ISO-10303-21;
HEADER;
/* Generated by software containing ST-Developer
 * from STEP Tools, Inc. (www.steptools.com) 
 */

FILE_DESCRIPTION(
/* description */ (''),
/* implementation_level */ '2;1');

FILE_NAME(
/* name */ 'End_Cap(Mirror).step',
/* time_stamp */ '2026-10-05T11:01:41-07:00',
/* author */ (''),
/* organization */ (''),
/* preprocessor_version */ 'ST-DEVELOPER v20.2',
/* originating_system */ 'Autodesk Translation Framework v15.15.0.0',
/* authorisation */ '');

FILE_SCHEMA (('AUTOMOTIVE_DESIGN { 1 0 10303 214 3 1 1 }'));
ENDSEC;

DATA;
#10=MECHANICAL_DESIGN_GEOMETRIC_PRESENTATION_REPRESENTATION('',(#2145),#215609);
#161=B_SPLINE_SURFACE_WITH_KNOTS('',3,3,((#207102,#207103,#207104,#207105,
#207106,#207107,#207108,#207109,#207110,#207111,#207112,#207113,#207114,
#207115,#207116,#207117,#207118,#207119,#207120,#207121,#207122,#207123,
#207124,#207125,#207126,#207127,#207128,#207129,#207130,#207131,#207132,
#207133,#207134,#207135,#207136,#207137,#207138,#207139,#207140,#207141,
#207142,#207143,#207144,#207145,#207146,#207147,#207148,#207149,#207150,
#207151,#207152,#207153,#207154,#207155),(#207156,#207157,#207158,#207159,
#207160,#207161,#207162,#207163,#207164,#207165,#207166,#207167,#207168,
#207169,#207170,#207171,#207172,#207173,#207174,#207175,#207176,#207177,
#207178,#207179,#207180,#207181,#207182,#207183,#207184,#207185,#207186,
#207187,#207188,#207189,#207190,#207191,#207192,#207193,#207194,#207195,
#207196,#207197,#207198,#207199,#207200,#207201,#207202,#207203,#207204,
#207205,#207206,#207207,#207208,#207209),(#207210,#207211,#207212,#207213,
#207214,#207215,#207216,#207217,#207218,#207219,#207220,#207221,#207222,
#207223,#207224,#207225,#207226,#207227,#207228,#207229,#207230,#207231,
#207232,#207233,#207234,#207235,#207236,#207237,#207238,#207239,#207240,
#207241,#207242,#207243,#207244,#207245,#207246,#207247,#207248,#207249,
#207250,#207251,#207252,#207253,#207254,#207255,#207256,#207257,#207258,
#207259,#207260,#207261,#207262,#207263),(#207264,#207265,#207266,#207267,
#207268,#207269,#207270,#207271,#207272,#207273,#207274,#207275,#207276,
#207277,#207278,#207279,#207280,#207281,#207282,#207283,#207284,#207285,
#207286,#207287,#207288,#207289,#207290,#207291,#207292,#207293,#207294,
#207295,#207296,#207297,#207298,#207299,#207300,#207301,#207302,#207303,
#207304,#207305,#207306,#207307,#207308,#207309,#207310,#207311,#207312,
#207313,#207314,#207315,#207316,#207317)),.UNSPECIFIED.,.F.,.F.,.F.,(4,
4),(4,1,1,1,1,1,1,1,1,1,1,1,1,1,1,1,1,1,1,1,1,1,1,1,1,1,1,1,1,1,1,1,1,1,
1,1,1,1,1,1,1,1,1,1,1,1,1,1,1,1,1,4),(-0.000616514442677502,0.096936516137423),
(11.8528940954716,12.340290362188,12.8276378599491,13.3149853577101,13.8023328554711,
14.2896803532321,14.7770278509931,15.2643753487541,15.7517228465151,16.2390703442761,
16.7264178420371,17.2137653397981,17.7011128375591,18.1884603353201,18.6758078330811,
19.1631553308421,19.6505028286031,20.1378503263641,20.6251978241251,21.1125453218861,
21.5998928196471,22.0872403174081,22.5745878151691,23.0619353129301,23.5492828106911,
24.5239778062131,25.4986728017351,26.4733677972571,26.9607152950181,27.4480627927791,
27.9354102905401,28.4227577883011,28.9101052860621,29.3974527838231,29.8848002815841,
30.3721477793451,30.8594952771061,31.3468427748671,31.8341902726282,32.3215377703892,
32.8088852681502,33.2962327659112,33.7835802636722,34.2709277614332,34.7582752591942,
35.2456227569552,35.7329702547162,36.2203177524772,36.7076652502382,37.1950127479992,
37.6823602457602,38.1697077435212),.UNSPECIFIED.);
#162=B_SPLINE_SURFACE_WITH_KNOTS('',3,3,((#207524,#207525,#207526,#207527,
#207528,#207529,#207530,#207531,#207532,#207533,#207534,#207535,#207536,
#207537,#207538,#207539,#207540,#207541,#207542,#207543,#207544,#207545,
#207546,#207547,#207548,#207549,#207550,#207551,#207552,#207553,#207554,
#207555,#207556,#207557,#207558,#207559,#207560,#207561,#207562,#207563,
#207564,#207565,#207566,#207567,#207568,#207569,#207570,#207571,#207572,
#207573,#207574,#207575,#207576,#207577),(#207578,#207579,#207580,#207581,
#207582,#207583,#207584,#207585,#207586,#207587,#207588,#207589,#207590,
#207591,#207592,#207593,#207594,#207595,#207596,#207597,#207598,#207599,
#207600,#207601,#207602,#207603,#207604,#207605,#207606,#207607,#207608,
#207609,#207610,#207611,#207612,#207613,#207614,#207615,#207616,#207617,
#207618,#207619,#207620,#207621,#207622,#207623,#207624,#207625,#207626,
#207627,#207628,#207629,#207630,#207631),(#207632,#207633,#207634,#207635,
#207636,#207637,#207638,#207639,#207640,#207641,#207642,#207643,#207644,
#207645,#207646,#207647,#207648,#207649,#207650,#207651,#207652,#207653,
#207654,#207655,#207656,#207657,#207658,#207659,#207660,#207661,#207662,
#207663,#207664,#207665,#207666,#207667,#207668,#207669,#207670,#207671,
#207672,#207673,#207674,#207675,#207676,#207677,#207678,#207679,#207680,
#207681,#207682,#207683,#207684,#207685),(#207686,#207687,#207688,#207689,
#207690,#207691,#207692,#207693,#207694,#207695,#207696,#207697,#207698,
#207699,#207700,#207701,#207702,#207703,#207704,#207705,#207706,#207707,
#207708,#207709,#207710,#207711,#207712,#207713,#207714,#207715,#207716,
#207717,#207718,#207719,#207720,#207721,#207722,#207723,#207724,#207725,
#207726,#207727,#207728,#207729,#207730,#207731,#207732,#207733,#207734,
#207735,#207736,#207737,#207738,#207739)),.UNSPECIFIED.,.F.,.F.,.F.,(4,
4),(4,1,1,1,1,1,1,1,1,1,1,1,1,1,1,1,1,1,1,1,1,1,1,1,1,1,1,1,1,1,1,1,1,1,
1,1,1,1,1,1,1,1,1,1,1,1,1,1,1,1,1,4),(-0.000403550678892824,0.0971495250489538),
(14.399609326548,14.886956824309,15.37430432207,15.861651819831,16.348999317592,
16.836346815353,17.323694313114,17.811041810875,18.298389308636,18.785736806397,
19.273084304158,19.7604318019191,20.2477792996801,20.7351267974411,21.2224742952021,
21.7098217929631,22.1971692907241,22.6845167884851,23.1718642862461,23.6592117840071,
24.1465592817681,24.6339067795291,25.1212542772901,25.6086017750511,26.0959492728121,
27.0706442683341,28.0453392638561,29.0200342593781,29.5073817571391,29.9947292549001,
30.4820767526611,30.9694242504221,31.4567717481831,31.9441192459441,32.4314667437051,
32.9188142414661,33.4061617392271,33.8935092369881,34.3808567347491,34.8682042325101,
35.3555517302711,35.8428992280321,36.3302467257931,36.8175942235541,37.3049417213151,
37.7922892190762,38.2796367168372,38.7669842145982,39.2543317123592,39.7416792101202,
40.2290267078812,40.7164229770097),.UNSPECIFIED.);
#163=B_SPLINE_SURFACE_WITH_KNOTS('',3,3,((#207943,#207944,#207945,#207946,
#207947,#207948,#207949,#207950,#207951,#207952,#207953,#207954,#207955,
#207956,#207957,#207958,#207959,#207960,#207961,#207962,#207963,#207964,
#207965,#207966,#207967,#207968,#207969,#207970,#207971,#207972,#207973,
#207974,#207975,#207976,#207977,#207978,#207979,#207980,#207981,#207982,
#207983,#207984,#207985,#207986,#207987,#207988,#207989,#207990,#207991,
#207992,#207993,#207994,#207995,#207996),(#207997,#207998,#207999,#208000,
#208001,#208002,#208003,#208004,#208005,#208006,#208007,#208008,#208009,
#208010,#208011,#208012,#208013,#208014,#208015,#208016,#208017,#208018,
#208019,#208020,#208021,#208022,#208023,#208024,#208025,#208026,#208027,
#208028,#208029,#208030,#208031,#208032,#208033,#208034,#208035,#208036,
#208037,#208038,#208039,#208040,#208041,#208042,#208043,#208044,#208045,
#208046,#208047,#208048,#208049,#208050),(#208051,#208052,#208053,#208054,
#208055,#208056,#208057,#208058,#208059,#208060,#208061,#208062,#208063,
#208064,#208065,#208066,#208067,#208068,#208069,#208070,#208071,#208072,
#208073,#208074,#208075,#208076,#208077,#208078,#208079,#208080,#208081,
#208082,#208083,#208084,#208085,#208086,#208087,#208088,#208089,#208090,
#208091,#208092,#208093,#208094,#208095,#208096,#208097,#208098,#208099,
#208100,#208101,#208102,#208103,#208104),(#208105,#208106,#208107,#208108,
#208109,#208110,#208111,#208112,#208113,#208114,#208115,#208116,#208117,
#208118,#208119,#208120,#208121,#208122,#208123,#208124,#208125,#208126,
#208127,#208128,#208129,#208130,#208131,#208132,#208133,#208134,#208135,
#208136,#208137,#208138,#208139,#208140,#208141,#208142,#208143,#208144,
#208145,#208146,#208147,#208148,#208149,#208150,#208151,#208152,#208153,
#208154,#208155,#208156,#208157,#208158)),.UNSPECIFIED.,.F.,.F.,.F.,(4,
4),(4,1,1,1,1,1,1,1,1,1,1,1,1,1,1,1,1,1,1,1,1,1,1,1,1,1,1,1,1,1,1,1,1,1,
1,1,1,1,1,1,1,1,1,1,1,1,1,1,1,1,1,4),(-0.000616665549394816,0.0969365142669611),
(11.8528940858174,12.340290362188,12.827637859949,13.31498535771,13.802332855471,
14.289680353232,14.777027850993,15.264375348754,15.751722846515,16.239070344276,
16.7264178420371,17.2137653397981,17.7011128375591,18.1884603353201,18.6758078330811,
19.1631553308421,19.6505028286031,20.1378503263641,20.6251978241251,21.1125453218861,
21.5998928196471,22.0872403174081,22.5745878151691,23.0619353129301,23.5492828106911,
24.5239778062131,25.4986728017351,26.4733677972571,26.9607152950181,27.4480627927791,
27.9354102905401,28.4227577883011,28.9101052860621,29.3974527838231,29.8848002815841,
30.3721477793451,30.8594952771061,31.3468427748671,31.8341902726281,32.3215377703891,
32.8088852681501,33.2962327659111,33.7835802636721,34.2709277614331,34.7582752591941,
35.2456227569552,35.7329702547162,36.2203177524772,36.7076652502382,37.1950127479992,
37.6823602457602,38.1697077435212),.UNSPECIFIED.);
#164=B_SPLINE_SURFACE_WITH_KNOTS('',3,3,((#208368,#208369,#208370,#208371,
#208372,#208373,#208374,#208375,#208376,#208377,#208378,#208379,#208380,
#208381,#208382,#208383,#208384,#208385,#208386,#208387,#208388,#208389,
#208390,#208391,#208392,#208393,#208394,#208395,#208396,#208397,#208398,
#208399,#208400,#208401,#208402,#208403,#208404,#208405,#208406,#208407,
#208408,#208409,#208410,#208411,#208412,#208413,#208414,#208415,#208416,
#208417,#208418,#208419,#208420,#208421),(#208422,#208423,#208424,#208425,
#208426,#208427,#208428,#208429,#208430,#208431,#208432,#208433,#208434,
#208435,#208436,#208437,#208438,#208439,#208440,#208441,#208442,#208443,
#208444,#208445,#208446,#208447,#208448,#208449,#208450,#208451,#208452,
#208453,#208454,#208455,#208456,#208457,#208458,#208459,#208460,#208461,
#208462,#208463,#208464,#208465,#208466,#208467,#208468,#208469,#208470,
#208471,#208472,#208473,#208474,#208475),(#208476,#208477,#208478,#208479,
#208480,#208481,#208482,#208483,#208484,#208485,#208486,#208487,#208488,
#208489,#208490,#208491,#208492,#208493,#208494,#208495,#208496,#208497,
#208498,#208499,#208500,#208501,#208502,#208503,#208504,#208505,#208506,
#208507,#208508,#208509,#208510,#208511,#208512,#208513,#208514,#208515,
#208516,#208517,#208518,#208519,#208520,#208521,#208522,#208523,#208524,
#208525,#208526,#208527,#208528,#208529),(#208530,#208531,#208532,#208533,
#208534,#208535,#208536,#208537,#208538,#208539,#208540,#208541,#208542,
#208543,#208544,#208545,#208546,#208547,#208548,#208549,#208550,#208551,
#208552,#208553,#208554,#208555,#208556,#208557,#208558,#208559,#208560,
#208561,#208562,#208563,#208564,#208565,#208566,#208567,#208568,#208569,
#208570,#208571,#208572,#208573,#208574,#208575,#208576,#208577,#208578,
#208579,#208580,#208581,#208582,#208583)),.UNSPECIFIED.,.F.,.F.,.F.,(4,
4),(4,1,1,1,1,1,1,1,1,1,1,1,1,1,1,1,1,1,1,1,1,1,1,1,1,1,1,1,1,1,1,1,1,1,
1,1,1,1,1,1,1,1,1,1,1,1,1,1,1,1,1,4),(-0.000403548226902083,0.0971496961622332),
(14.399609326548,14.886956824309,15.37430432207,15.861651819831,16.348999317592,
16.836346815353,17.323694313114,17.811041810875,18.298389308636,18.785736806397,
19.273084304158,19.760431801919,20.24777929968,20.735126797441,21.222474295202,
21.709821792963,22.1971692907241,22.6845167884851,23.1718642862461,23.6592117840071,
24.1465592817681,24.6339067795291,25.1212542772901,25.6086017750511,26.0959492728121,
27.0706442683341,28.0453392638561,29.0200342593781,29.5073817571391,29.9947292549001,
30.4820767526611,30.9694242504221,31.4567717481831,31.9441192459441,32.4314667437051,
32.9188142414661,33.4061617392271,33.8935092369881,34.3808567347491,34.8682042325101,
35.3555517302711,35.8428992280321,36.3302467257931,36.8175942235541,37.3049417213151,
37.7922892190761,38.2796367168371,38.7669842145981,39.2543317123591,39.7416792101202,
40.2290267078812,40.7164229892059),.UNSPECIFIED.);
#165=B_SPLINE_SURFACE_WITH_KNOTS('',3,3,((#208796,#208797,#208798,#208799,
#208800,#208801,#208802,#208803,#208804,#208805,#208806,#208807,#208808,
#208809,#208810,#208811,#208812,#208813,#208814,#208815,#208816,#208817,
#208818,#208819,#208820,#208821,#208822,#208823,#208824,#208825,#208826,
#208827,#208828,#208829,#208830,#208831,#208832,#208833,#208834,#208835,
#208836,#208837,#208838,#208839,#208840,#208841,#208842,#208843,#208844,
#208845,#208846,#208847,#208848,#208849,#208850,#208851,#208852,#208853,
#208854,#208855,#208856,#208857,#208858,#208859,#208860,#208861,#208862,
#208863,#208864,#208865,#208866,#208867,#208868,#208869,#208870,#208871,
#208872,#208873,#208874,#208875,#208876,#208877,#208878,#208879,#208880,
#208881,#208882,#208883,#208884,#208885,#208886,#208887,#208888,#208889,
#208890,#208891,#208892,#208893,#208894,#208895,#208896,#208897,#208898,
#208899,#208900,#208901,#208902,#208903,#208904,#208905,#208906,#208907,
#208908,#208909,#208910,#208911,#208912,#208913,#208914,#208915,#208916,
#208917,#208918,#208919,#208920,#208921,#208922,#208923,#208924,#208925,
#208926,#208927,#208928,#208929,#208930,#208931,#208932,#208933,#208934,
#208935,#208936,#208937,#208938,#208939,#208940,#208941,#208942,#208943,
#208944,#208945,#208946,#208947,#208948,#208949,#208950,#208951,#208952,
#208953,#208954,#208955,#208956,#208957,#208958,#208959,#208960,#208961,
#208962,#208963,#208964,#208965,#208966,#208967,#208968,#208969,#208970,
#208971,#208972,#208973),(#208974,#208975,#208976,#208977,#208978,#208979,
#208980,#208981,#208982,#208983,#208984,#208985,#208986,#208987,#208988,
#208989,#208990,#208991,#208992,#208993,#208994,#208995,#208996,#208997,
#208998,#208999,#209000,#209001,#209002,#209003,#209004,#209005,#209006,
#209007,#209008,#209009,#209010,#209011,#209012,#209013,#209014,#209015,
#209016,#209017,#209018,#209019,#209020,#209021,#209022,#209023,#209024,
#209025,#209026,#209027,#209028,#209029,#209030,#209031,#209032,#209033,
#209034,#209035,#209036,#209037,#209038,#209039,#209040,#209041,#209042,
#209043,#209044,#209045,#209046,#209047,#209048,#209049,#209050,#209051,
#209052,#209053,#209054,#209055,#209056,#209057,#209058,#209059,#209060,
#209061,#209062,#209063,#209064,#209065,#209066,#209067,#209068,#209069,
#209070,#209071,#209072,#209073,#209074,#209075,#209076,#209077,#209078,
#209079,#209080,#209081,#209082,#209083,#209084,#209085,#209086,#209087,
#209088,#209089,#209090,#209091,#209092,#209093,#209094,#209095,#209096,
#209097,#209098,#209099,#209100,#209101,#209102,#209103,#209104,#209105,
#209106,#209107,#209108,#209109,#209110,#209111,#209112,#209113,#209114,
#209115,#209116,#209117,#209118,#209119,#209120,#209121,#209122,#209123,
#209124,#209125,#209126,#209127,#209128,#209129,#209130,#209131,#209132,
#209133,#209134,#209135,#209136,#209137,#209138,#209139,#209140,#209141,
#209142,#209143,#209144,#209145,#209146,#209147,#209148,#209149,#209150,
#209151),(#209152,#209153,#209154,#209155,#209156,#209157,#209158,#209159,
#209160,#209161,#209162,#209163,#209164,#209165,#209166,#209167,#209168,
#209169,#209170,#209171,#209172,#209173,#209174,#209175,#209176,#209177,
#209178,#209179,#209180,#209181,#209182,#209183,#209184,#209185,#209186,
#209187,#209188,#209189,#209190,#209191,#209192,#209193,#209194,#209195,
#209196,#209197,#209198,#209199,#209200,#209201,#209202,#209203,#209204,
#209205,#209206,#209207,#209208,#209209,#209210,#209211,#209212,#209213,
#209214,#209215,#209216,#209217,#209218,#209219,#209220,#209221,#209222,
#209223,#209224,#209225,#209226,#209227,#209228,#209229,#209230,#209231,
#209232,#209233,#209234,#209235,#209236,#209237,#209238,#209239,#209240,
#209241,#209242,#209243,#209244,#209245,#209246,#209247,#209248,#209249,
#209250,#209251,#209252,#209253,#209254,#209255,#209256,#209257,#209258,
#209259,#209260,#209261,#209262,#209263,#209264,#209265,#209266,#209267,
#209268,#209269,#209270,#209271,#209272,#209273,#209274,#209275,#209276,
#209277,#209278,#209279,#209280,#209281,#209282,#209283,#209284,#209285,
#209286,#209287,#209288,#209289,#209290,#209291,#209292,#209293,#209294,
#209295,#209296,#209297,#209298,#209299,#209300,#209301,#209302,#209303,
#209304,#209305,#209306,#209307,#209308,#209309,#209310,#209311,#209312,
#209313,#209314,#209315,#209316,#209317,#209318,#209319,#209320,#209321,
#209322,#209323,#209324,#209325,#209326,#209327,#209328,#209329),(#209330,
#209331,#209332,#209333,#209334,#209335,#209336,#209337,#209338,#209339,
#209340,#209341,#209342,#209343,#209344,#209345,#209346,#209347,#209348,
#209349,#209350,#209351,#209352,#209353,#209354,#209355,#209356,#209357,
#209358,#209359,#209360,#209361,#209362,#209363,#209364,#209365,#209366,
#209367,#209368,#209369,#209370,#209371,#209372,#209373,#209374,#209375,
#209376,#209377,#209378,#209379,#209380,#209381,#209382,#209383,#209384,
#209385,#209386,#209387,#209388,#209389,#209390,#209391,#209392,#209393,
#209394,#209395,#209396,#209397,#209398,#209399,#209400,#209401,#209402,
#209403,#209404,#209405,#209406,#209407,#209408,#209409,#209410,#209411,
#209412,#209413,#209414,#209415,#209416,#209417,#209418,#209419,#209420,
#209421,#209422,#209423,#209424,#209425,#209426,#209427,#209428,#209429,
#209430,#209431,#209432,#209433,#209434,#209435,#209436,#209437,#209438,
#209439,#209440,#209441,#209442,#209443,#209444,#209445,#209446,#209447,
#209448,#209449,#209450,#209451,#209452,#209453,#209454,#209455,#209456,
#209457,#209458,#209459,#209460,#209461,#209462,#209463,#209464,#209465,
#209466,#209467,#209468,#209469,#209470,#209471,#209472,#209473,#209474,
#209475,#209476,#209477,#209478,#209479,#209480,#209481,#209482,#209483,
#209484,#209485,#209486,#209487,#209488,#209489,#209490,#209491,#209492,
#209493,#209494,#209495,#209496,#209497,#209498,#209499,#209500,#209501,
#209502,#209503,#209504,#209505,#209506,#209507)),.UNSPECIFIED.,.F.,.F.,
 .F.,(4,4),(4,1,1,1,1,1,1,1,1,1,1,1,1,1,1,1,1,1,1,1,1,1,1,1,1,1,1,1,1,1,
1,1,1,1,1,1,1,1,1,1,1,1,1,1,1,1,1,1,1,1,1,1,1,1,1,1,1,1,1,1,1,1,1,1,1,1,
1,1,1,1,1,1,1,1,1,1,1,1,1,1,1,1,1,1,1,1,1,1,1,1,1,1,1,1,1,1,1,1,1,1,1,1,
1,1,1,1,1,1,1,1,1,1,1,1,1,1,1,1,1,1,1,1,1,1,1,1,1,1,1,1,1,1,1,1,1,1,1,1,
1,1,1,1,1,1,1,1,1,1,1,1,1,1,1,1,1,1,1,1,1,1,1,1,1,1,1,1,1,1,1,1,1,1,1,1,
1,4),(-0.000439606948779753,0.0515314320759051),(11.8664846275776,12.8657606844883,
13.8645971344502,14.8634335844121,15.8622700343739,16.8611064843358,17.8599429342977,
18.8587793842595,19.8576158342214,20.8564522841833,21.8552887341452,22.854125184107,
23.8529616340689,24.8517980840308,25.8506345339927,26.8494709839545,27.8483074339164,
28.8471438838783,29.8459803338402,30.844816783802,31.8436532337639,32.8424896837258,
33.8413261336877,34.8401625836495,35.8389990336114,36.8378354835733,37.8366719335352,
38.835508383497,39.8343448334589,40.8331812834208,41.8320177333826,42.8308541833445,
43.8296906333064,44.8285270832683,45.8273635332301,46.826199983192,47.8250364331539,
48.8238728831158,49.8227093330776,50.8215457830395,51.8203822330014,52.8192186829633,
53.8180551329251,54.816891582887,55.8157280328489,56.8145644828108,57.8134009327726,
58.8122373827345,59.8110738326964,60.8099102826583,61.8087467326201,62.807583182582,
63.8064196325439,64.8052560825058,65.8040925324676,66.8029289824295,67.8017654323914,
68.8006018823532,69.7994383323151,70.798274782277,71.7971112322389,72.7959476822007,
73.7947841321626,74.7936205821245,75.7924570320864,76.7912934820482,77.7901299320101,
78.788966381972,79.7878028319339,80.7866392818957,81.7854757318576,82.7843121818195,
83.7831486317814,84.7819850817432,85.7808215317051,86.779657981667,87.7784944316288,
88.7773308815907,89.7761673315526,90.7750037815145,91.7738402314764,92.7726766814382,
93.7715131314001,94.770349581362,95.7691860313238,96.7680224812857,97.7668589312476,
98.7656953812095,99.7645318311714,100.763368281133,101.762204731095,102.761041181057,
103.759877631019,104.758714080981,105.757550530943,106.756386980904,107.755223430866,
108.754059880828,109.75289633079,110.751732780752,111.750569230714,112.749405680676,
113.748242130638,114.747078580599,115.745915030561,116.744751480523,117.743587930485,
118.742424380447,119.741260830409,120.740097280371,121.738933730333,122.737770180294,
123.736606630256,124.735443080218,125.73427953018,126.733115980142,127.731952430104,
128.730788880066,129.729625330028,130.728461779989,131.727298229951,132.726134679913,
133.724971129875,134.723807579837,135.722644029799,136.721480479761,137.720316929723,
138.719153379684,139.717989829646,140.716826279608,141.71566272957,142.714499179532,
143.713335629494,144.712172079456,145.711008529418,146.709844979379,147.708681429341,
148.707517879303,149.706354329265,150.705190779227,151.704027229189,152.702863679151,
153.701700129113,154.700536579074,155.699373029036,156.698209478998,157.69704592896,
158.695882378922,159.694718828884,160.693555278846,161.692391728808,162.691228178769,
163.690064628731,164.688901078693,165.687737528655,166.686573978617,167.685410428579,
168.684246878541,169.683083328503,170.681919778464,171.680756228426,172.679592678388,
173.67842912835,174.677265578312,175.676102028274,176.674938478236,177.673774928198,
178.672611378159,179.671447828121,180.670284278083,181.669120728045,182.667957178007,
183.666793627969,184.665630077931,185.664466527893,186.663302977854),
 .UNSPECIFIED.);
#166=B_SPLINE_SURFACE_WITH_KNOTS('',3,3,((#209596,#209597,#209598,#209599,
#209600,#209601,#209602,#209603,#209604,#209605,#209606,#209607,#209608,
#209609,#209610,#209611,#209612,#209613,#209614,#209615,#209616,#209617,
#209618,#209619,#209620,#209621,#209622,#209623,#209624,#209625,#209626,
#209627,#209628,#209629,#209630,#209631,#209632,#209633,#209634,#209635,
#209636,#209637,#209638,#209639,#209640,#209641,#209642,#209643,#209644,
#209645,#209646,#209647,#209648,#209649,#209650,#209651,#209652,#209653,
#209654,#209655,#209656,#209657,#209658,#209659,#209660,#209661,#209662,
#209663,#209664,#209665,#209666,#209667,#209668,#209669,#209670,#209671,
#209672,#209673,#209674,#209675,#209676,#209677,#209678,#209679,#209680,
#209681,#209682,#209683,#209684,#209685,#209686,#209687,#209688,#209689,
#209690,#209691,#209692,#209693,#209694,#209695,#209696,#209697,#209698,
#209699,#209700,#209701,#209702,#209703,#209704,#209705,#209706,#209707,
#209708,#209709,#209710,#209711,#209712,#209713,#209714,#209715,#209716,
#209717,#209718,#209719,#209720,#209721,#209722,#209723,#209724,#209725,
#209726,#209727,#209728,#209729,#209730,#209731,#209732,#209733,#209734,
#209735,#209736,#209737,#209738,#209739,#209740,#209741,#209742,#209743,
#209744,#209745,#209746,#209747,#209748,#209749,#209750,#209751,#209752,
#209753,#209754,#209755,#209756,#209757,#209758,#209759,#209760,#209761,
#209762,#209763,#209764,#209765,#209766,#209767,#209768,#209769,#209770,
#209771,#209772,#209773),(#209774,#209775,#209776,#209777,#209778,#209779,
#209780,#209781,#209782,#209783,#209784,#209785,#209786,#209787,#209788,
#209789,#209790,#209791,#209792,#209793,#209794,#209795,#209796,#209797,
#209798,#209799,#209800,#209801,#209802,#209803,#209804,#209805,#209806,
#209807,#209808,#209809,#209810,#209811,#209812,#209813,#209814,#209815,
#209816,#209817,#209818,#209819,#209820,#209821,#209822,#209823,#209824,
#209825,#209826,#209827,#209828,#209829,#209830,#209831,#209832,#209833,
#209834,#209835,#209836,#209837,#209838,#209839,#209840,#209841,#209842,
#209843,#209844,#209845,#209846,#209847,#209848,#209849,#209850,#209851,
#209852,#209853,#209854,#209855,#209856,#209857,#209858,#209859,#209860,
#209861,#209862,#209863,#209864,#209865,#209866,#209867,#209868,#209869,
#209870,#209871,#209872,#209873,#209874,#209875,#209876,#209877,#209878,
#209879,#209880,#209881,#209882,#209883,#209884,#209885,#209886,#209887,
#209888,#209889,#209890,#209891,#209892,#209893,#209894,#209895,#209896,
#209897,#209898,#209899,#209900,#209901,#209902,#209903,#209904,#209905,
#209906,#209907,#209908,#209909,#209910,#209911,#209912,#209913,#209914,
#209915,#209916,#209917,#209918,#209919,#209920,#209921,#209922,#209923,
#209924,#209925,#209926,#209927,#209928,#209929,#209930,#209931,#209932,
#209933,#209934,#209935,#209936,#209937,#209938,#209939,#209940,#209941,
#209942,#209943,#209944,#209945,#209946,#209947,#209948,#209949,#209950,
#209951),(#209952,#209953,#209954,#209955,#209956,#209957,#209958,#209959,
#209960,#209961,#209962,#209963,#209964,#209965,#209966,#209967,#209968,
#209969,#209970,#209971,#209972,#209973,#209974,#209975,#209976,#209977,
#209978,#209979,#209980,#209981,#209982,#209983,#209984,#209985,#209986,
#209987,#209988,#209989,#209990,#209991,#209992,#209993,#209994,#209995,
#209996,#209997,#209998,#209999,#210000,#210001,#210002,#210003,#210004,
#210005,#210006,#210007,#210008,#210009,#210010,#210011,#210012,#210013,
#210014,#210015,#210016,#210017,#210018,#210019,#210020,#210021,#210022,
#210023,#210024,#210025,#210026,#210027,#210028,#210029,#210030,#210031,
#210032,#210033,#210034,#210035,#210036,#210037,#210038,#210039,#210040,
#210041,#210042,#210043,#210044,#210045,#210046,#210047,#210048,#210049,
#210050,#210051,#210052,#210053,#210054,#210055,#210056,#210057,#210058,
#210059,#210060,#210061,#210062,#210063,#210064,#210065,#210066,#210067,
#210068,#210069,#210070,#210071,#210072,#210073,#210074,#210075,#210076,
#210077,#210078,#210079,#210080,#210081,#210082,#210083,#210084,#210085,
#210086,#210087,#210088,#210089,#210090,#210091,#210092,#210093,#210094,
#210095,#210096,#210097,#210098,#210099,#210100,#210101,#210102,#210103,
#210104,#210105,#210106,#210107,#210108,#210109,#210110,#210111,#210112,
#210113,#210114,#210115,#210116,#210117,#210118,#210119,#210120,#210121,
#210122,#210123,#210124,#210125,#210126,#210127,#210128,#210129),(#210130,
#210131,#210132,#210133,#210134,#210135,#210136,#210137,#210138,#210139,
#210140,#210141,#210142,#210143,#210144,#210145,#210146,#210147,#210148,
#210149,#210150,#210151,#210152,#210153,#210154,#210155,#210156,#210157,
#210158,#210159,#210160,#210161,#210162,#210163,#210164,#210165,#210166,
#210167,#210168,#210169,#210170,#210171,#210172,#210173,#210174,#210175,
#210176,#210177,#210178,#210179,#210180,#210181,#210182,#210183,#210184,
#210185,#210186,#210187,#210188,#210189,#210190,#210191,#210192,#210193,
#210194,#210195,#210196,#210197,#210198,#210199,#210200,#210201,#210202,
#210203,#210204,#210205,#210206,#210207,#210208,#210209,#210210,#210211,
#210212,#210213,#210214,#210215,#210216,#210217,#210218,#210219,#210220,
#210221,#210222,#210223,#210224,#210225,#210226,#210227,#210228,#210229,
#210230,#210231,#210232,#210233,#210234,#210235,#210236,#210237,#210238,
#210239,#210240,#210241,#210242,#210243,#210244,#210245,#210246,#210247,
#210248,#210249,#210250,#210251,#210252,#210253,#210254,#210255,#210256,
#210257,#210258,#210259,#210260,#210261,#210262,#210263,#210264,#210265,
#210266,#210267,#210268,#210269,#210270,#210271,#210272,#210273,#210274,
#210275,#210276,#210277,#210278,#210279,#210280,#210281,#210282,#210283,
#210284,#210285,#210286,#210287,#210288,#210289,#210290,#210291,#210292,
#210293,#210294,#210295,#210296,#210297,#210298,#210299,#210300,#210301,
#210302,#210303,#210304,#210305,#210306,#210307)),.UNSPECIFIED.,.F.,.F.,
 .F.,(4,4),(4,1,1,1,1,1,1,1,1,1,1,1,1,1,1,1,1,1,1,1,1,1,1,1,1,1,1,1,1,1,
1,1,1,1,1,1,1,1,1,1,1,1,1,1,1,1,1,1,1,1,1,1,1,1,1,1,1,1,1,1,1,1,1,1,1,1,
1,1,1,1,1,1,1,1,1,1,1,1,1,1,1,1,1,1,1,1,1,1,1,1,1,1,1,1,1,1,1,1,1,1,1,1,
1,1,1,1,1,1,1,1,1,1,1,1,1,1,1,1,1,1,1,1,1,1,1,1,1,1,1,1,1,1,1,1,1,1,1,1,
1,1,1,1,1,1,1,1,1,1,1,1,1,1,1,1,1,1,1,1,1,1,1,1,1,1,1,1,1,1,1,1,1,1,1,1,
1,4),(-0.000378201108638619,0.051592837406338),(14.3986268518925,15.3974633018543,
16.3962997518162,17.3951362017781,18.39397265174,19.3928091017018,20.3916455516637,
21.3904820016256,22.3893184515875,23.3881549015493,24.3869913515112,25.3858278014731,
26.3846642514349,27.3835007013968,28.3823371513587,29.3811736013206,30.3800100512824,
31.3788465012443,32.3776829512062,33.3765194011681,34.3753558511299,35.3741923010918,
36.3730287510537,37.3718652010156,38.3707016509774,39.3695381009393,40.3683745509012,
41.3672110008631,42.3660474508249,43.3648839007868,44.3637203507487,45.3625568007106,
46.3613932506724,47.3602297006343,48.3590661505962,49.3579026005581,50.3567390505199,
51.3555755004818,52.3544119504437,53.3532484004055,54.3520848503674,55.3509213003293,
56.3497577502912,57.348594200253,58.3474306502149,59.3462671001768,60.3451035501387,
61.3439400001005,62.3427764500624,63.3416129000243,64.3404493499862,65.339285799948,
66.3381222499099,67.3369586998718,68.3357951498337,69.3346315997955,70.3334680497574,
71.3323044997193,72.3311409496812,73.329977399643,74.3288138496049,75.3276502995668,
76.3264867495287,77.3253231994905,78.3241596494524,79.3229960994143,80.3218325493762,
81.320668999338,82.3195054492999,83.3183418992618,84.3171783492237,85.3160147991855,
86.3148512491474,87.3136876991093,88.3125241490712,89.311360599033,90.3101970489949,
91.3090334989568,92.3078699489186,93.3067063988805,94.3055428488424,95.3043792988043,
96.3032157487661,97.302052198728,98.3008886486899,99.2997250986518,100.298561548614,
101.297397998576,102.296234448537,103.295070898499,104.293907348461,105.292743798423,
106.291580248385,107.290416698347,108.289253148309,109.288089598271,110.286926048232,
111.285762498194,112.284598948156,113.283435398118,114.28227184808,115.281108298042,
116.279944748004,117.278781197966,118.277617647927,119.276454097889,120.275290547851,
121.274126997813,122.272963447775,123.271799897737,124.270636347699,125.26947279766,
126.268309247622,127.267145697584,128.265982147546,129.264818597508,130.26365504747,
131.262491497432,132.261327947394,133.260164397355,134.259000847317,135.257837297279,
136.256673747241,137.255510197203,138.254346647165,139.253183097127,140.252019547089,
141.25085599705,142.249692447012,143.248528896974,144.247365346936,145.246201796898,
146.24503824686,147.243874696822,148.242711146784,149.241547596745,150.240384046707,
151.239220496669,152.238056946631,153.236893396593,154.235729846555,155.234566296517,
156.233402746479,157.23223919644,158.231075646402,159.229912096364,160.228748546326,
161.227584996288,162.22642144625,163.225257896212,164.224094346174,165.222930796135,
166.221767246097,167.220603696059,168.219440146021,169.218276595983,170.217113045945,
171.215949495907,172.214785945869,173.21362239583,174.212458845792,175.211295295754,
176.210131745716,177.208968195678,178.20780464564,179.206641095602,180.205477545564,
181.204313995525,182.203150445487,183.201986895449,184.200823345411,185.199659795373,
186.198496245335,187.197332695297,188.196169145259,189.195445198776),
 .UNSPECIFIED.);
#167=B_SPLINE_SURFACE_WITH_KNOTS('',3,3,((#210399,#210400,#210401,#210402,
#210403,#210404,#210405,#210406,#210407,#210408,#210409,#210410,#210411,
#210412,#210413,#210414,#210415,#210416,#210417,#210418,#210419,#210420,
#210421,#210422,#210423,#210424,#210425,#210426,#210427,#210428,#210429,
#210430,#210431,#210432,#210433,#210434,#210435,#210436,#210437,#210438,
#210439,#210440,#210441,#210442,#210443,#210444,#210445,#210446,#210447,
#210448,#210449,#210450,#210451,#210452,#210453,#210454,#210455,#210456,
#210457,#210458,#210459,#210460,#210461,#210462,#210463,#210464,#210465,
#210466,#210467,#210468,#210469,#210470,#210471,#210472,#210473,#210474,
#210475,#210476,#210477,#210478,#210479,#210480,#210481,#210482,#210483,
#210484,#210485,#210486,#210487,#210488,#210489,#210490,#210491,#210492,
#210493,#210494,#210495,#210496,#210497,#210498,#210499,#210500,#210501,
#210502,#210503,#210504,#210505,#210506,#210507,#210508,#210509,#210510,
#210511,#210512,#210513,#210514,#210515,#210516,#210517,#210518,#210519,
#210520,#210521,#210522,#210523,#210524,#210525,#210526,#210527,#210528,
#210529,#210530,#210531,#210532,#210533,#210534,#210535,#210536,#210537,
#210538,#210539,#210540,#210541,#210542,#210543,#210544,#210545,#210546,
#210547,#210548,#210549,#210550,#210551,#210552,#210553,#210554,#210555,
#210556,#210557,#210558,#210559,#210560,#210561,#210562,#210563,#210564,
#210565,#210566,#210567,#210568,#210569,#210570,#210571,#210572,#210573,
#210574,#210575,#210576),(#210577,#210578,#210579,#210580,#210581,#210582,
#210583,#210584,#210585,#210586,#210587,#210588,#210589,#210590,#210591,
#210592,#210593,#210594,#210595,#210596,#210597,#210598,#210599,#210600,
#210601,#210602,#210603,#210604,#210605,#210606,#210607,#210608,#210609,
#210610,#210611,#210612,#210613,#210614,#210615,#210616,#210617,#210618,
#210619,#210620,#210621,#210622,#210623,#210624,#210625,#210626,#210627,
#210628,#210629,#210630,#210631,#210632,#210633,#210634,#210635,#210636,
#210637,#210638,#210639,#210640,#210641,#210642,#210643,#210644,#210645,
#210646,#210647,#210648,#210649,#210650,#210651,#210652,#210653,#210654,
#210655,#210656,#210657,#210658,#210659,#210660,#210661,#210662,#210663,
#210664,#210665,#210666,#210667,#210668,#210669,#210670,#210671,#210672,
#210673,#210674,#210675,#210676,#210677,#210678,#210679,#210680,#210681,
#210682,#210683,#210684,#210685,#210686,#210687,#210688,#210689,#210690,
#210691,#210692,#210693,#210694,#210695,#210696,#210697,#210698,#210699,
#210700,#210701,#210702,#210703,#210704,#210705,#210706,#210707,#210708,
#210709,#210710,#210711,#210712,#210713,#210714,#210715,#210716,#210717,
#210718,#210719,#210720,#210721,#210722,#210723,#210724,#210725,#210726,
#210727,#210728,#210729,#210730,#210731,#210732,#210733,#210734,#210735,
#210736,#210737,#210738,#210739,#210740,#210741,#210742,#210743,#210744,
#210745,#210746,#210747,#210748,#210749,#210750,#210751,#210752,#210753,
#210754),(#210755,#210756,#210757,#210758,#210759,#210760,#210761,#210762,
#210763,#210764,#210765,#210766,#210767,#210768,#210769,#210770,#210771,
#210772,#210773,#210774,#210775,#210776,#210777,#210778,#210779,#210780,
#210781,#210782,#210783,#210784,#210785,#210786,#210787,#210788,#210789,
#210790,#210791,#210792,#210793,#210794,#210795,#210796,#210797,#210798,
#210799,#210800,#210801,#210802,#210803,#210804,#210805,#210806,#210807,
#210808,#210809,#210810,#210811,#210812,#210813,#210814,#210815,#210816,
#210817,#210818,#210819,#210820,#210821,#210822,#210823,#210824,#210825,
#210826,#210827,#210828,#210829,#210830,#210831,#210832,#210833,#210834,
#210835,#210836,#210837,#210838,#210839,#210840,#210841,#210842,#210843,
#210844,#210845,#210846,#210847,#210848,#210849,#210850,#210851,#210852,
#210853,#210854,#210855,#210856,#210857,#210858,#210859,#210860,#210861,
#210862,#210863,#210864,#210865,#210866,#210867,#210868,#210869,#210870,
#210871,#210872,#210873,#210874,#210875,#210876,#210877,#210878,#210879,
#210880,#210881,#210882,#210883,#210884,#210885,#210886,#210887,#210888,
#210889,#210890,#210891,#210892,#210893,#210894,#210895,#210896,#210897,
#210898,#210899,#210900,#210901,#210902,#210903,#210904,#210905,#210906,
#210907,#210908,#210909,#210910,#210911,#210912,#210913,#210914,#210915,
#210916,#210917,#210918,#210919,#210920,#210921,#210922,#210923,#210924,
#210925,#210926,#210927,#210928,#210929,#210930,#210931,#210932),(#210933,
#210934,#210935,#210936,#210937,#210938,#210939,#210940,#210941,#210942,
#210943,#210944,#210945,#210946,#210947,#210948,#210949,#210950,#210951,
#210952,#210953,#210954,#210955,#210956,#210957,#210958,#210959,#210960,
#210961,#210962,#210963,#210964,#210965,#210966,#210967,#210968,#210969,
#210970,#210971,#210972,#210973,#210974,#210975,#210976,#210977,#210978,
#210979,#210980,#210981,#210982,#210983,#210984,#210985,#210986,#210987,
#210988,#210989,#210990,#210991,#210992,#210993,#210994,#210995,#210996,
#210997,#210998,#210999,#211000,#211001,#211002,#211003,#211004,#211005,
#211006,#211007,#211008,#211009,#211010,#211011,#211012,#211013,#211014,
#211015,#211016,#211017,#211018,#211019,#211020,#211021,#211022,#211023,
#211024,#211025,#211026,#211027,#211028,#211029,#211030,#211031,#211032,
#211033,#211034,#211035,#211036,#211037,#211038,#211039,#211040,#211041,
#211042,#211043,#211044,#211045,#211046,#211047,#211048,#211049,#211050,
#211051,#211052,#211053,#211054,#211055,#211056,#211057,#211058,#211059,
#211060,#211061,#211062,#211063,#211064,#211065,#211066,#211067,#211068,
#211069,#211070,#211071,#211072,#211073,#211074,#211075,#211076,#211077,
#211078,#211079,#211080,#211081,#211082,#211083,#211084,#211085,#211086,
#211087,#211088,#211089,#211090,#211091,#211092,#211093,#211094,#211095,
#211096,#211097,#211098,#211099,#211100,#211101,#211102,#211103,#211104,
#211105,#211106,#211107,#211108,#211109,#211110)),.UNSPECIFIED.,.F.,.F.,
 .F.,(4,4),(4,1,1,1,1,1,1,1,1,1,1,1,1,1,1,1,1,1,1,1,1,1,1,1,1,1,1,1,1,1,
1,1,1,1,1,1,1,1,1,1,1,1,1,1,1,1,1,1,1,1,1,1,1,1,1,1,1,1,1,1,1,1,1,1,1,1,
1,1,1,1,1,1,1,1,1,1,1,1,1,1,1,1,1,1,1,1,1,1,1,1,1,1,1,1,1,1,1,1,1,1,1,1,
1,1,1,1,1,1,1,1,1,1,1,1,1,1,1,1,1,1,1,1,1,1,1,1,1,1,1,1,1,1,1,1,1,1,1,1,
1,1,1,1,1,1,1,1,1,1,1,1,1,1,1,1,1,1,1,1,1,1,1,1,1,1,1,1,1,1,1,1,1,1,1,1,
1,4),(-0.000439572862182752,0.0515314610720388),(11.8664846616642,12.8657606844883,
13.8645971344502,14.8634335844121,15.8622700343739,16.8611064843358,17.8599429342977,
18.8587793842595,19.8576158342214,20.8564522841833,21.8552887341452,22.854125184107,
23.8529616340689,24.8517980840308,25.8506345339927,26.8494709839545,27.8483074339164,
28.8471438838783,29.8459803338402,30.844816783802,31.8436532337639,32.8424896837258,
33.8413261336877,34.8401625836495,35.8389990336114,36.8378354835733,37.8366719335352,
38.835508383497,39.8343448334589,40.8331812834208,41.8320177333826,42.8308541833445,
43.8296906333064,44.8285270832683,45.8273635332301,46.826199983192,47.8250364331539,
48.8238728831158,49.8227093330776,50.8215457830395,51.8203822330014,52.8192186829633,
53.8180551329251,54.816891582887,55.8157280328489,56.8145644828108,57.8134009327726,
58.8122373827345,59.8110738326964,60.8099102826583,61.8087467326201,62.807583182582,
63.8064196325439,64.8052560825058,65.8040925324676,66.8029289824295,67.8017654323914,
68.8006018823532,69.7994383323151,70.798274782277,71.7971112322389,72.7959476822007,
73.7947841321626,74.7936205821245,75.7924570320864,76.7912934820482,77.7901299320101,
78.788966381972,79.7878028319339,80.7866392818957,81.7854757318576,82.7843121818195,
83.7831486317814,84.7819850817432,85.7808215317051,86.779657981667,87.7784944316289,
88.7773308815907,89.7761673315526,90.7750037815145,91.7738402314764,92.7726766814382,
93.7715131314001,94.770349581362,95.7691860313239,96.7680224812857,97.7668589312476,
98.7656953812095,99.7645318311714,100.763368281133,101.762204731095,102.761041181057,
103.759877631019,104.758714080981,105.757550530943,106.756386980904,107.755223430866,
108.754059880828,109.75289633079,110.751732780752,111.750569230714,112.749405680676,
113.748242130638,114.747078580599,115.745915030561,116.744751480523,117.743587930485,
118.742424380447,119.741260830409,120.740097280371,121.738933730333,122.737770180294,
123.736606630256,124.735443080218,125.73427953018,126.733115980142,127.731952430104,
128.730788880066,129.729625330028,130.728461779989,131.727298229951,132.726134679913,
133.724971129875,134.723807579837,135.722644029799,136.721480479761,137.720316929723,
138.719153379684,139.717989829646,140.716826279608,141.71566272957,142.714499179532,
143.713335629494,144.712172079456,145.711008529418,146.709844979379,147.708681429341,
148.707517879303,149.706354329265,150.705190779227,151.704027229189,152.702863679151,
153.701700129113,154.700536579074,155.699373029036,156.698209478998,157.69704592896,
158.695882378922,159.694718828884,160.693555278846,161.692391728808,162.691228178769,
163.690064628731,164.688901078693,165.687737528655,166.686573978617,167.685410428579,
168.684246878541,169.683083328503,170.681919778464,171.680756228426,172.679592678388,
173.67842912835,174.677265578312,175.676102028274,176.674938478236,177.673774928198,
178.672611378159,179.671447828121,180.670284278083,181.669120728045,182.667957178007,
183.666793627969,184.665630077931,185.664466527893,186.663302977854),
 .UNSPECIFIED.);
#168=B_SPLINE_SURFACE_WITH_KNOTS('',3,3,((#211199,#211200,#211201,#211202,
#211203,#211204,#211205,#211206,#211207,#211208,#211209,#211210,#211211,
#211212,#211213,#211214,#211215,#211216,#211217,#211218,#211219,#211220,
#211221,#211222,#211223,#211224,#211225,#211226,#211227,#211228,#211229,
#211230,#211231,#211232,#211233,#211234,#211235,#211236,#211237,#211238,
#211239,#211240,#211241,#211242,#211243,#211244,#211245,#211246,#211247,
#211248,#211249,#211250,#211251,#211252,#211253,#211254,#211255,#211256,
#211257,#211258,#211259,#211260,#211261,#211262,#211263,#211264,#211265,
#211266,#211267,#211268,#211269,#211270,#211271,#211272,#211273,#211274,
#211275,#211276,#211277,#211278,#211279,#211280,#211281,#211282,#211283,
#211284,#211285,#211286,#211287,#211288,#211289,#211290,#211291,#211292,
#211293,#211294,#211295,#211296,#211297,#211298,#211299,#211300,#211301,
#211302,#211303,#211304,#211305,#211306,#211307,#211308,#211309,#211310,
#211311,#211312,#211313,#211314,#211315,#211316,#211317,#211318,#211319,
#211320,#211321,#211322,#211323,#211324,#211325,#211326,#211327,#211328,
#211329,#211330,#211331,#211332,#211333,#211334,#211335,#211336,#211337,
#211338,#211339,#211340,#211341,#211342,#211343,#211344,#211345,#211346,
#211347,#211348,#211349,#211350,#211351,#211352,#211353,#211354,#211355,
#211356,#211357,#211358,#211359,#211360,#211361,#211362,#211363,#211364,
#211365,#211366,#211367,#211368,#211369,#211370,#211371,#211372,#211373,
#211374,#211375,#211376),(#211377,#211378,#211379,#211380,#211381,#211382,
#211383,#211384,#211385,#211386,#211387,#211388,#211389,#211390,#211391,
#211392,#211393,#211394,#211395,#211396,#211397,#211398,#211399,#211400,
#211401,#211402,#211403,#211404,#211405,#211406,#211407,#211408,#211409,
#211410,#211411,#211412,#211413,#211414,#211415,#211416,#211417,#211418,
#211419,#211420,#211421,#211422,#211423,#211424,#211425,#211426,#211427,
#211428,#211429,#211430,#211431,#211432,#211433,#211434,#211435,#211436,
#211437,#211438,#211439,#211440,#211441,#211442,#211443,#211444,#211445,
#211446,#211447,#211448,#211449,#211450,#211451,#211452,#211453,#211454,
#211455,#211456,#211457,#211458,#211459,#211460,#211461,#211462,#211463,
#211464,#211465,#211466,#211467,#211468,#211469,#211470,#211471,#211472,
#211473,#211474,#211475,#211476,#211477,#211478,#211479,#211480,#211481,
#211482,#211483,#211484,#211485,#211486,#211487,#211488,#211489,#211490,
#211491,#211492,#211493,#211494,#211495,#211496,#211497,#211498,#211499,
#211500,#211501,#211502,#211503,#211504,#211505,#211506,#211507,#211508,
#211509,#211510,#211511,#211512,#211513,#211514,#211515,#211516,#211517,
#211518,#211519,#211520,#211521,#211522,#211523,#211524,#211525,#211526,
#211527,#211528,#211529,#211530,#211531,#211532,#211533,#211534,#211535,
#211536,#211537,#211538,#211539,#211540,#211541,#211542,#211543,#211544,
#211545,#211546,#211547,#211548,#211549,#211550,#211551,#211552,#211553,
#211554),(#211555,#211556,#211557,#211558,#211559,#211560,#211561,#211562,
#211563,#211564,#211565,#211566,#211567,#211568,#211569,#211570,#211571,
#211572,#211573,#211574,#211575,#211576,#211577,#211578,#211579,#211580,
#211581,#211582,#211583,#211584,#211585,#211586,#211587,#211588,#211589,
#211590,#211591,#211592,#211593,#211594,#211595,#211596,#211597,#211598,
#211599,#211600,#211601,#211602,#211603,#211604,#211605,#211606,#211607,
#211608,#211609,#211610,#211611,#211612,#211613,#211614,#211615,#211616,
#211617,#211618,#211619,#211620,#211621,#211622,#211623,#211624,#211625,
#211626,#211627,#211628,#211629,#211630,#211631,#211632,#211633,#211634,
#211635,#211636,#211637,#211638,#211639,#211640,#211641,#211642,#211643,
#211644,#211645,#211646,#211647,#211648,#211649,#211650,#211651,#211652,
#211653,#211654,#211655,#211656,#211657,#211658,#211659,#211660,#211661,
#211662,#211663,#211664,#211665,#211666,#211667,#211668,#211669,#211670,
#211671,#211672,#211673,#211674,#211675,#211676,#211677,#211678,#211679,
#211680,#211681,#211682,#211683,#211684,#211685,#211686,#211687,#211688,
#211689,#211690,#211691,#211692,#211693,#211694,#211695,#211696,#211697,
#211698,#211699,#211700,#211701,#211702,#211703,#211704,#211705,#211706,
#211707,#211708,#211709,#211710,#211711,#211712,#211713,#211714,#211715,
#211716,#211717,#211718,#211719,#211720,#211721,#211722,#211723,#211724,
#211725,#211726,#211727,#211728,#211729,#211730,#211731,#211732),(#211733,
#211734,#211735,#211736,#211737,#211738,#211739,#211740,#211741,#211742,
#211743,#211744,#211745,#211746,#211747,#211748,#211749,#211750,#211751,
#211752,#211753,#211754,#211755,#211756,#211757,#211758,#211759,#211760,
#211761,#211762,#211763,#211764,#211765,#211766,#211767,#211768,#211769,
#211770,#211771,#211772,#211773,#211774,#211775,#211776,#211777,#211778,
#211779,#211780,#211781,#211782,#211783,#211784,#211785,#211786,#211787,
#211788,#211789,#211790,#211791,#211792,#211793,#211794,#211795,#211796,
#211797,#211798,#211799,#211800,#211801,#211802,#211803,#211804,#211805,
#211806,#211807,#211808,#211809,#211810,#211811,#211812,#211813,#211814,
#211815,#211816,#211817,#211818,#211819,#211820,#211821,#211822,#211823,
#211824,#211825,#211826,#211827,#211828,#211829,#211830,#211831,#211832,
#211833,#211834,#211835,#211836,#211837,#211838,#211839,#211840,#211841,
#211842,#211843,#211844,#211845,#211846,#211847,#211848,#211849,#211850,
#211851,#211852,#211853,#211854,#211855,#211856,#211857,#211858,#211859,
#211860,#211861,#211862,#211863,#211864,#211865,#211866,#211867,#211868,
#211869,#211870,#211871,#211872,#211873,#211874,#211875,#211876,#211877,
#211878,#211879,#211880,#211881,#211882,#211883,#211884,#211885,#211886,
#211887,#211888,#211889,#211890,#211891,#211892,#211893,#211894,#211895,
#211896,#211897,#211898,#211899,#211900,#211901,#211902,#211903,#211904,
#211905,#211906,#211907,#211908,#211909,#211910)),.UNSPECIFIED.,.F.,.F.,
 .F.,(4,4),(4,1,1,1,1,1,1,1,1,1,1,1,1,1,1,1,1,1,1,1,1,1,1,1,1,1,1,1,1,1,
1,1,1,1,1,1,1,1,1,1,1,1,1,1,1,1,1,1,1,1,1,1,1,1,1,1,1,1,1,1,1,1,1,1,1,1,
1,1,1,1,1,1,1,1,1,1,1,1,1,1,1,1,1,1,1,1,1,1,1,1,1,1,1,1,1,1,1,1,1,1,1,1,
1,1,1,1,1,1,1,1,1,1,1,1,1,1,1,1,1,1,1,1,1,1,1,1,1,1,1,1,1,1,1,1,1,1,1,1,
1,1,1,1,1,1,1,1,1,1,1,1,1,1,1,1,1,1,1,1,1,1,1,1,1,1,1,1,1,1,1,1,1,1,1,1,
1,4),(-0.000378192696997217,0.0515928473073539),(14.3986268518925,15.3974633018543,
16.3962997518162,17.3951362017781,18.39397265174,19.3928091017018,20.3916455516637,
21.3904820016256,22.3893184515875,23.3881549015493,24.3869913515112,25.3858278014731,
26.3846642514349,27.3835007013968,28.3823371513587,29.3811736013206,30.3800100512824,
31.3788465012443,32.3776829512062,33.3765194011681,34.3753558511299,35.3741923010918,
36.3730287510537,37.3718652010156,38.3707016509774,39.3695381009393,40.3683745509012,
41.3672110008631,42.3660474508249,43.3648839007868,44.3637203507487,45.3625568007106,
46.3613932506724,47.3602297006343,48.3590661505962,49.3579026005581,50.3567390505199,
51.3555755004818,52.3544119504437,53.3532484004055,54.3520848503674,55.3509213003293,
56.3497577502912,57.348594200253,58.3474306502149,59.3462671001768,60.3451035501387,
61.3439400001005,62.3427764500624,63.3416129000243,64.3404493499862,65.339285799948,
66.3381222499099,67.3369586998718,68.3357951498337,69.3346315997955,70.3334680497574,
71.3323044997193,72.3311409496812,73.329977399643,74.3288138496049,75.3276502995668,
76.3264867495287,77.3253231994905,78.3241596494524,79.3229960994143,80.3218325493762,
81.320668999338,82.3195054492999,83.3183418992618,84.3171783492237,85.3160147991855,
86.3148512491474,87.3136876991093,88.3125241490712,89.311360599033,90.3101970489949,
91.3090334989568,92.3078699489186,93.3067063988805,94.3055428488424,95.3043792988043,
96.3032157487661,97.302052198728,98.3008886486899,99.2997250986518,100.298561548614,
101.297397998576,102.296234448537,103.295070898499,104.293907348461,105.292743798423,
106.291580248385,107.290416698347,108.289253148309,109.288089598271,110.286926048232,
111.285762498194,112.284598948156,113.283435398118,114.28227184808,115.281108298042,
116.279944748004,117.278781197966,118.277617647927,119.276454097889,120.275290547851,
121.274126997813,122.272963447775,123.271799897737,124.270636347699,125.26947279766,
126.268309247622,127.267145697584,128.265982147546,129.264818597508,130.26365504747,
131.262491497432,132.261327947394,133.260164397355,134.259000847317,135.257837297279,
136.256673747241,137.255510197203,138.254346647165,139.253183097127,140.252019547089,
141.25085599705,142.249692447012,143.248528896974,144.247365346936,145.246201796898,
146.24503824686,147.243874696822,148.242711146784,149.241547596745,150.240384046707,
151.239220496669,152.238056946631,153.236893396593,154.235729846555,155.234566296517,
156.233402746479,157.23223919644,158.231075646402,159.229912096364,160.228748546326,
161.227584996288,162.22642144625,163.225257896212,164.224094346174,165.222930796135,
166.221767246097,167.220603696059,168.219440146021,169.218276595983,170.217113045945,
171.215949495907,172.214785945869,173.21362239583,174.212458845792,175.211295295754,
176.210131745716,177.208968195678,178.20780464564,179.206641095602,180.205477545564,
181.204313995525,182.203150445487,183.201986895449,184.200823345411,185.199659795373,
186.198496245335,187.197332695297,188.196169145259,189.195445208677),
 .UNSPECIFIED.);
#169=B_SPLINE_SURFACE_WITH_KNOTS('',3,3,((#211999,#212000,#212001,#212002,
#212003,#212004,#212005,#212006,#212007,#212008,#212009,#212010,#212011,
#212012,#212013,#212014,#212015,#212016,#212017,#212018,#212019,#212020,
#212021,#212022,#212023,#212024,#212025,#212026,#212027,#212028,#212029,
#212030,#212031,#212032,#212033,#212034,#212035,#212036,#212037,#212038,
#212039,#212040,#212041,#212042,#212043,#212044,#212045,#212046,#212047,
#212048,#212049,#212050,#212051,#212052,#212053,#212054,#212055,#212056,
#212057,#212058,#212059,#212060,#212061,#212062,#212063,#212064,#212065,
#212066,#212067,#212068,#212069,#212070,#212071,#212072,#212073,#212074,
#212075,#212076,#212077,#212078,#212079,#212080,#212081,#212082,#212083,
#212084,#212085,#212086,#212087,#212088,#212089,#212090,#212091,#212092,
#212093,#212094,#212095,#212096,#212097,#212098,#212099,#212100,#212101,
#212102,#212103,#212104,#212105,#212106,#212107,#212108,#212109,#212110,
#212111,#212112,#212113,#212114,#212115,#212116,#212117,#212118,#212119,
#212120,#212121,#212122,#212123,#212124,#212125,#212126,#212127,#212128,
#212129,#212130,#212131,#212132,#212133,#212134,#212135,#212136,#212137,
#212138,#212139,#212140,#212141,#212142,#212143,#212144,#212145,#212146,
#212147,#212148,#212149,#212150,#212151,#212152,#212153,#212154,#212155,
#212156,#212157,#212158,#212159,#212160,#212161,#212162,#212163,#212164,
#212165,#212166,#212167,#212168,#212169,#212170,#212171,#212172,#212173,
#212174,#212175,#212176),(#212177,#212178,#212179,#212180,#212181,#212182,
#212183,#212184,#212185,#212186,#212187,#212188,#212189,#212190,#212191,
#212192,#212193,#212194,#212195,#212196,#212197,#212198,#212199,#212200,
#212201,#212202,#212203,#212204,#212205,#212206,#212207,#212208,#212209,
#212210,#212211,#212212,#212213,#212214,#212215,#212216,#212217,#212218,
#212219,#212220,#212221,#212222,#212223,#212224,#212225,#212226,#212227,
#212228,#212229,#212230,#212231,#212232,#212233,#212234,#212235,#212236,
#212237,#212238,#212239,#212240,#212241,#212242,#212243,#212244,#212245,
#212246,#212247,#212248,#212249,#212250,#212251,#212252,#212253,#212254,
#212255,#212256,#212257,#212258,#212259,#212260,#212261,#212262,#212263,
#212264,#212265,#212266,#212267,#212268,#212269,#212270,#212271,#212272,
#212273,#212274,#212275,#212276,#212277,#212278,#212279,#212280,#212281,
#212282,#212283,#212284,#212285,#212286,#212287,#212288,#212289,#212290,
#212291,#212292,#212293,#212294,#212295,#212296,#212297,#212298,#212299,
#212300,#212301,#212302,#212303,#212304,#212305,#212306,#212307,#212308,
#212309,#212310,#212311,#212312,#212313,#212314,#212315,#212316,#212317,
#212318,#212319,#212320,#212321,#212322,#212323,#212324,#212325,#212326,
#212327,#212328,#212329,#212330,#212331,#212332,#212333,#212334,#212335,
#212336,#212337,#212338,#212339,#212340,#212341,#212342,#212343,#212344,
#212345,#212346,#212347,#212348,#212349,#212350,#212351,#212352,#212353,
#212354),(#212355,#212356,#212357,#212358,#212359,#212360,#212361,#212362,
#212363,#212364,#212365,#212366,#212367,#212368,#212369,#212370,#212371,
#212372,#212373,#212374,#212375,#212376,#212377,#212378,#212379,#212380,
#212381,#212382,#212383,#212384,#212385,#212386,#212387,#212388,#212389,
#212390,#212391,#212392,#212393,#212394,#212395,#212396,#212397,#212398,
#212399,#212400,#212401,#212402,#212403,#212404,#212405,#212406,#212407,
#212408,#212409,#212410,#212411,#212412,#212413,#212414,#212415,#212416,
#212417,#212418,#212419,#212420,#212421,#212422,#212423,#212424,#212425,
#212426,#212427,#212428,#212429,#212430,#212431,#212432,#212433,#212434,
#212435,#212436,#212437,#212438,#212439,#212440,#212441,#212442,#212443,
#212444,#212445,#212446,#212447,#212448,#212449,#212450,#212451,#212452,
#212453,#212454,#212455,#212456,#212457,#212458,#212459,#212460,#212461,
#212462,#212463,#212464,#212465,#212466,#212467,#212468,#212469,#212470,
#212471,#212472,#212473,#212474,#212475,#212476,#212477,#212478,#212479,
#212480,#212481,#212482,#212483,#212484,#212485,#212486,#212487,#212488,
#212489,#212490,#212491,#212492,#212493,#212494,#212495,#212496,#212497,
#212498,#212499,#212500,#212501,#212502,#212503,#212504,#212505,#212506,
#212507,#212508,#212509,#212510,#212511,#212512,#212513,#212514,#212515,
#212516,#212517,#212518,#212519,#212520,#212521,#212522,#212523,#212524,
#212525,#212526,#212527,#212528,#212529,#212530,#212531,#212532),(#212533,
#212534,#212535,#212536,#212537,#212538,#212539,#212540,#212541,#212542,
#212543,#212544,#212545,#212546,#212547,#212548,#212549,#212550,#212551,
#212552,#212553,#212554,#212555,#212556,#212557,#212558,#212559,#212560,
#212561,#212562,#212563,#212564,#212565,#212566,#212567,#212568,#212569,
#212570,#212571,#212572,#212573,#212574,#212575,#212576,#212577,#212578,
#212579,#212580,#212581,#212582,#212583,#212584,#212585,#212586,#212587,
#212588,#212589,#212590,#212591,#212592,#212593,#212594,#212595,#212596,
#212597,#212598,#212599,#212600,#212601,#212602,#212603,#212604,#212605,
#212606,#212607,#212608,#212609,#212610,#212611,#212612,#212613,#212614,
#212615,#212616,#212617,#212618,#212619,#212620,#212621,#212622,#212623,
#212624,#212625,#212626,#212627,#212628,#212629,#212630,#212631,#212632,
#212633,#212634,#212635,#212636,#212637,#212638,#212639,#212640,#212641,
#212642,#212643,#212644,#212645,#212646,#212647,#212648,#212649,#212650,
#212651,#212652,#212653,#212654,#212655,#212656,#212657,#212658,#212659,
#212660,#212661,#212662,#212663,#212664,#212665,#212666,#212667,#212668,
#212669,#212670,#212671,#212672,#212673,#212674,#212675,#212676,#212677,
#212678,#212679,#212680,#212681,#212682,#212683,#212684,#212685,#212686,
#212687,#212688,#212689,#212690,#212691,#212692,#212693,#212694,#212695,
#212696,#212697,#212698,#212699,#212700,#212701,#212702,#212703,#212704,
#212705,#212706,#212707,#212708,#212709,#212710)),.UNSPECIFIED.,.F.,.F.,
 .F.,(4,4),(4,1,1,1,1,1,1,1,1,1,1,1,1,1,1,1,1,1,1,1,1,1,1,1,1,1,1,1,1,1,
1,1,1,1,1,1,1,1,1,1,1,1,1,1,1,1,1,1,1,1,1,1,1,1,1,1,1,1,1,1,1,1,1,1,1,1,
1,1,1,1,1,1,1,1,1,1,1,1,1,1,1,1,1,1,1,1,1,1,1,1,1,1,1,1,1,1,1,1,1,1,1,1,
1,1,1,1,1,1,1,1,1,1,1,1,1,1,1,1,1,1,1,1,1,1,1,1,1,1,1,1,1,1,1,1,1,1,1,1,
1,1,1,1,1,1,1,1,1,1,1,1,1,1,1,1,1,1,1,1,1,1,1,1,1,1,1,1,1,1,1,1,1,1,1,1,
1,4),(-0.000439572128272221,0.0515314616970906),(11.8664846623981,12.8657606844883,
13.8645971344502,14.8634335844121,15.8622700343739,16.8611064843358,17.8599429342977,
18.8587793842596,19.8576158342214,20.8564522841833,21.8552887341452,22.854125184107,
23.8529616340689,24.8517980840308,25.8506345339927,26.8494709839545,27.8483074339164,
28.8471438838783,29.8459803338402,30.844816783802,31.8436532337639,32.8424896837258,
33.8413261336877,34.8401625836495,35.8389990336114,36.8378354835733,37.8366719335352,
38.835508383497,39.8343448334589,40.8331812834208,41.8320177333827,42.8308541833445,
43.8296906333064,44.8285270832683,45.8273635332302,46.826199983192,47.8250364331539,
48.8238728831158,49.8227093330777,50.8215457830395,51.8203822330014,52.8192186829633,
53.8180551329252,54.816891582887,55.8157280328489,56.8145644828108,57.8134009327727,
58.8122373827345,59.8110738326964,60.8099102826583,61.8087467326202,62.807583182582,
63.8064196325439,64.8052560825058,65.8040925324676,66.8029289824295,67.8017654323914,
68.8006018823533,69.7994383323151,70.798274782277,71.7971112322389,72.7959476822008,
73.7947841321626,74.7936205821245,75.7924570320864,76.7912934820483,77.7901299320101,
78.788966381972,79.7878028319339,80.7866392818958,81.7854757318576,82.7843121818195,
83.7831486317814,84.7819850817433,85.7808215317051,86.779657981667,87.7784944316289,
88.7773308815908,89.7761673315526,90.7750037815145,91.7738402314764,92.7726766814383,
93.7715131314001,94.770349581362,95.7691860313239,96.7680224812858,97.7668589312476,
98.7656953812095,99.7645318311714,100.763368281133,101.762204731095,102.761041181057,
103.759877631019,104.758714080981,105.757550530943,106.756386980905,107.755223430866,
108.754059880828,109.75289633079,110.751732780752,111.750569230714,112.749405680676,
113.748242130638,114.747078580599,115.745915030561,116.744751480523,117.743587930485,
118.742424380447,119.741260830409,120.740097280371,121.738933730333,122.737770180294,
123.736606630256,124.735443080218,125.73427953018,126.733115980142,127.731952430104,
128.730788880066,129.729625330028,130.728461779989,131.727298229951,132.726134679913,
133.724971129875,134.723807579837,135.722644029799,136.721480479761,137.720316929723,
138.719153379684,139.717989829646,140.716826279608,141.71566272957,142.714499179532,
143.713335629494,144.712172079456,145.711008529418,146.709844979379,147.708681429341,
148.707517879303,149.706354329265,150.705190779227,151.704027229189,152.702863679151,
153.701700129113,154.700536579074,155.699373029036,156.698209478998,157.69704592896,
158.695882378922,159.694718828884,160.693555278846,161.692391728808,162.691228178769,
163.690064628731,164.688901078693,165.687737528655,166.686573978617,167.685410428579,
168.684246878541,169.683083328503,170.681919778464,171.680756228426,172.679592678388,
173.67842912835,174.677265578312,175.676102028274,176.674938478236,177.673774928198,
178.672611378159,179.671447828121,180.670284278083,181.669120728045,182.667957178007,
183.666793627969,184.665630077931,185.664466527893,186.663302977854),
 .UNSPECIFIED.);
#170=B_SPLINE_SURFACE_WITH_KNOTS('',3,3,((#212799,#212800,#212801,#212802,
#212803,#212804,#212805,#212806,#212807,#212808,#212809,#212810,#212811,
#212812,#212813,#212814,#212815,#212816,#212817,#212818,#212819,#212820,
#212821,#212822,#212823,#212824,#212825,#212826,#212827,#212828,#212829,
#212830,#212831,#212832,#212833,#212834,#212835,#212836,#212837,#212838,
#212839,#212840,#212841,#212842,#212843,#212844,#212845,#212846,#212847,
#212848,#212849,#212850,#212851,#212852,#212853,#212854,#212855,#212856,
#212857,#212858,#212859,#212860,#212861,#212862,#212863,#212864,#212865,
#212866,#212867,#212868,#212869,#212870,#212871,#212872,#212873,#212874,
#212875,#212876,#212877,#212878,#212879,#212880,#212881,#212882,#212883,
#212884,#212885,#212886,#212887,#212888,#212889,#212890,#212891,#212892,
#212893,#212894,#212895,#212896,#212897,#212898,#212899,#212900,#212901,
#212902,#212903,#212904,#212905,#212906,#212907,#212908,#212909,#212910,
#212911,#212912,#212913,#212914,#212915,#212916,#212917,#212918,#212919,
#212920,#212921,#212922,#212923,#212924,#212925,#212926,#212927,#212928,
#212929,#212930,#212931,#212932,#212933,#212934,#212935,#212936,#212937,
#212938,#212939,#212940,#212941,#212942,#212943,#212944,#212945,#212946,
#212947,#212948,#212949,#212950,#212951,#212952,#212953,#212954,#212955,
#212956,#212957,#212958,#212959,#212960,#212961,#212962,#212963,#212964,
#212965,#212966,#212967,#212968,#212969,#212970,#212971,#212972,#212973,
#212974,#212975,#212976),(#212977,#212978,#212979,#212980,#212981,#212982,
#212983,#212984,#212985,#212986,#212987,#212988,#212989,#212990,#212991,
#212992,#212993,#212994,#212995,#212996,#212997,#212998,#212999,#213000,
#213001,#213002,#213003,#213004,#213005,#213006,#213007,#213008,#213009,
#213010,#213011,#213012,#213013,#213014,#213015,#213016,#213017,#213018,
#213019,#213020,#213021,#213022,#213023,#213024,#213025,#213026,#213027,
#213028,#213029,#213030,#213031,#213032,#213033,#213034,#213035,#213036,
#213037,#213038,#213039,#213040,#213041,#213042,#213043,#213044,#213045,
#213046,#213047,#213048,#213049,#213050,#213051,#213052,#213053,#213054,
#213055,#213056,#213057,#213058,#213059,#213060,#213061,#213062,#213063,
#213064,#213065,#213066,#213067,#213068,#213069,#213070,#213071,#213072,
#213073,#213074,#213075,#213076,#213077,#213078,#213079,#213080,#213081,
#213082,#213083,#213084,#213085,#213086,#213087,#213088,#213089,#213090,
#213091,#213092,#213093,#213094,#213095,#213096,#213097,#213098,#213099,
#213100,#213101,#213102,#213103,#213104,#213105,#213106,#213107,#213108,
#213109,#213110,#213111,#213112,#213113,#213114,#213115,#213116,#213117,
#213118,#213119,#213120,#213121,#213122,#213123,#213124,#213125,#213126,
#213127,#213128,#213129,#213130,#213131,#213132,#213133,#213134,#213135,
#213136,#213137,#213138,#213139,#213140,#213141,#213142,#213143,#213144,
#213145,#213146,#213147,#213148,#213149,#213150,#213151,#213152,#213153,
#213154),(#213155,#213156,#213157,#213158,#213159,#213160,#213161,#213162,
#213163,#213164,#213165,#213166,#213167,#213168,#213169,#213170,#213171,
#213172,#213173,#213174,#213175,#213176,#213177,#213178,#213179,#213180,
#213181,#213182,#213183,#213184,#213185,#213186,#213187,#213188,#213189,
#213190,#213191,#213192,#213193,#213194,#213195,#213196,#213197,#213198,
#213199,#213200,#213201,#213202,#213203,#213204,#213205,#213206,#213207,
#213208,#213209,#213210,#213211,#213212,#213213,#213214,#213215,#213216,
#213217,#213218,#213219,#213220,#213221,#213222,#213223,#213224,#213225,
#213226,#213227,#213228,#213229,#213230,#213231,#213232,#213233,#213234,
#213235,#213236,#213237,#213238,#213239,#213240,#213241,#213242,#213243,
#213244,#213245,#213246,#213247,#213248,#213249,#213250,#213251,#213252,
#213253,#213254,#213255,#213256,#213257,#213258,#213259,#213260,#213261,
#213262,#213263,#213264,#213265,#213266,#213267,#213268,#213269,#213270,
#213271,#213272,#213273,#213274,#213275,#213276,#213277,#213278,#213279,
#213280,#213281,#213282,#213283,#213284,#213285,#213286,#213287,#213288,
#213289,#213290,#213291,#213292,#213293,#213294,#213295,#213296,#213297,
#213298,#213299,#213300,#213301,#213302,#213303,#213304,#213305,#213306,
#213307,#213308,#213309,#213310,#213311,#213312,#213313,#213314,#213315,
#213316,#213317,#213318,#213319,#213320,#213321,#213322,#213323,#213324,
#213325,#213326,#213327,#213328,#213329,#213330,#213331,#213332),(#213333,
#213334,#213335,#213336,#213337,#213338,#213339,#213340,#213341,#213342,
#213343,#213344,#213345,#213346,#213347,#213348,#213349,#213350,#213351,
#213352,#213353,#213354,#213355,#213356,#213357,#213358,#213359,#213360,
#213361,#213362,#213363,#213364,#213365,#213366,#213367,#213368,#213369,
#213370,#213371,#213372,#213373,#213374,#213375,#213376,#213377,#213378,
#213379,#213380,#213381,#213382,#213383,#213384,#213385,#213386,#213387,
#213388,#213389,#213390,#213391,#213392,#213393,#213394,#213395,#213396,
#213397,#213398,#213399,#213400,#213401,#213402,#213403,#213404,#213405,
#213406,#213407,#213408,#213409,#213410,#213411,#213412,#213413,#213414,
#213415,#213416,#213417,#213418,#213419,#213420,#213421,#213422,#213423,
#213424,#213425,#213426,#213427,#213428,#213429,#213430,#213431,#213432,
#213433,#213434,#213435,#213436,#213437,#213438,#213439,#213440,#213441,
#213442,#213443,#213444,#213445,#213446,#213447,#213448,#213449,#213450,
#213451,#213452,#213453,#213454,#213455,#213456,#213457,#213458,#213459,
#213460,#213461,#213462,#213463,#213464,#213465,#213466,#213467,#213468,
#213469,#213470,#213471,#213472,#213473,#213474,#213475,#213476,#213477,
#213478,#213479,#213480,#213481,#213482,#213483,#213484,#213485,#213486,
#213487,#213488,#213489,#213490,#213491,#213492,#213493,#213494,#213495,
#213496,#213497,#213498,#213499,#213500,#213501,#213502,#213503,#213504,
#213505,#213506,#213507,#213508,#213509,#213510)),.UNSPECIFIED.,.F.,.F.,
 .F.,(4,4),(4,1,1,1,1,1,1,1,1,1,1,1,1,1,1,1,1,1,1,1,1,1,1,1,1,1,1,1,1,1,
1,1,1,1,1,1,1,1,1,1,1,1,1,1,1,1,1,1,1,1,1,1,1,1,1,1,1,1,1,1,1,1,1,1,1,1,
1,1,1,1,1,1,1,1,1,1,1,1,1,1,1,1,1,1,1,1,1,1,1,1,1,1,1,1,1,1,1,1,1,1,1,1,
1,1,1,1,1,1,1,1,1,1,1,1,1,1,1,1,1,1,1,1,1,1,1,1,1,1,1,1,1,1,1,1,1,1,1,1,
1,1,1,1,1,1,1,1,1,1,1,1,1,1,1,1,1,1,1,1,1,1,1,1,1,1,1,1,1,1,1,1,1,1,1,1,
1,4),(-0.000378196170333693,0.0515928432182127),(14.3986268518925,15.3974633018543,
16.3962997518162,17.3951362017781,18.39397265174,19.3928091017018,20.3916455516637,
21.3904820016256,22.3893184515875,23.3881549015493,24.3869913515112,25.3858278014731,
26.384664251435,27.3835007013968,28.3823371513587,29.3811736013206,30.3800100512825,
31.3788465012443,32.3776829512062,33.3765194011681,34.37535585113,35.3741923010918,
36.3730287510537,37.3718652010156,38.3707016509774,39.3695381009393,40.3683745509012,
41.3672110008631,42.3660474508249,43.3648839007868,44.3637203507487,45.3625568007106,
46.3613932506724,47.3602297006343,48.3590661505962,49.3579026005581,50.3567390505199,
51.3555755004818,52.3544119504437,53.3532484004056,54.3520848503674,55.3509213003293,
56.3497577502912,57.3485942002531,58.3474306502149,59.3462671001768,60.3451035501387,
61.3439400001006,62.3427764500624,63.3416129000243,64.3404493499862,65.3392857999481,
66.3381222499099,67.3369586998718,68.3357951498337,69.3346315997956,70.3334680497574,
71.3323044997193,72.3311409496812,73.3299773996431,74.3288138496049,75.3276502995668,
76.3264867495287,77.3253231994906,78.3241596494524,79.3229960994143,80.3218325493762,
81.3206689993381,82.3195054492999,83.3183418992618,84.3171783492237,85.3160147991856,
86.3148512491474,87.3136876991093,88.3125241490712,89.3113605990331,90.3101970489949,
91.3090334989568,92.3078699489187,93.3067063988806,94.3055428488424,95.3043792988043,
96.3032157487662,97.302052198728,98.3008886486899,99.2997250986518,100.298561548614,
101.297397998576,102.296234448537,103.295070898499,104.293907348461,105.292743798423,
106.291580248385,107.290416698347,108.289253148309,109.288089598271,110.286926048232,
111.285762498194,112.284598948156,113.283435398118,114.28227184808,115.281108298042,
116.279944748004,117.278781197966,118.277617647927,119.276454097889,120.275290547851,
121.274126997813,122.272963447775,123.271799897737,124.270636347699,125.269472797661,
126.268309247622,127.267145697584,128.265982147546,129.264818597508,130.26365504747,
131.262491497432,132.261327947394,133.260164397356,134.259000847317,135.257837297279,
136.256673747241,137.255510197203,138.254346647165,139.253183097127,140.252019547089,
141.250855997051,142.249692447012,143.248528896974,144.247365346936,145.246201796898,
146.24503824686,147.243874696822,148.242711146784,149.241547596746,150.240384046707,
151.239220496669,152.238056946631,153.236893396593,154.235729846555,155.234566296517,
156.233402746479,157.232239196441,158.231075646402,159.229912096364,160.228748546326,
161.227584996288,162.22642144625,163.225257896212,164.224094346174,165.222930796136,
166.221767246097,167.220603696059,168.219440146021,169.218276595983,170.217113045945,
171.215949495907,172.214785945869,173.21362239583,174.212458845792,175.211295295754,
176.210131745716,177.208968195678,178.20780464564,179.206641095602,180.205477545564,
181.204313995525,182.203150445487,183.201986895449,184.200823345411,185.199659795373,
186.198496245335,187.197332695297,188.196169145259,189.195445204588),
 .UNSPECIFIED.);
#171=B_SPLINE_SURFACE_WITH_KNOTS('',3,3,((#213599,#213600,#213601,#213602,
#213603,#213604,#213605,#213606,#213607,#213608,#213609,#213610,#213611,
#213612,#213613,#213614,#213615,#213616,#213617,#213618,#213619,#213620,
#213621,#213622,#213623,#213624,#213625,#213626,#213627,#213628,#213629,
#213630,#213631,#213632,#213633,#213634,#213635,#213636,#213637,#213638,
#213639,#213640,#213641,#213642,#213643,#213644,#213645,#213646,#213647,
#213648,#213649,#213650,#213651,#213652,#213653,#213654,#213655,#213656,
#213657,#213658,#213659,#213660,#213661,#213662,#213663,#213664,#213665,
#213666,#213667,#213668,#213669,#213670,#213671,#213672,#213673,#213674,
#213675,#213676,#213677,#213678,#213679,#213680,#213681,#213682,#213683,
#213684,#213685,#213686,#213687,#213688,#213689,#213690,#213691,#213692,
#213693,#213694,#213695,#213696,#213697,#213698,#213699,#213700,#213701,
#213702,#213703,#213704,#213705,#213706,#213707,#213708,#213709,#213710,
#213711,#213712,#213713,#213714,#213715,#213716,#213717,#213718,#213719,
#213720,#213721,#213722,#213723,#213724,#213725,#213726,#213727,#213728,
#213729,#213730,#213731,#213732,#213733,#213734,#213735,#213736,#213737,
#213738,#213739,#213740,#213741,#213742,#213743,#213744,#213745,#213746,
#213747,#213748,#213749,#213750,#213751,#213752,#213753,#213754,#213755,
#213756,#213757,#213758,#213759,#213760,#213761,#213762,#213763,#213764,
#213765,#213766,#213767,#213768,#213769,#213770,#213771,#213772,#213773,
#213774,#213775,#213776),(#213777,#213778,#213779,#213780,#213781,#213782,
#213783,#213784,#213785,#213786,#213787,#213788,#213789,#213790,#213791,
#213792,#213793,#213794,#213795,#213796,#213797,#213798,#213799,#213800,
#213801,#213802,#213803,#213804,#213805,#213806,#213807,#213808,#213809,
#213810,#213811,#213812,#213813,#213814,#213815,#213816,#213817,#213818,
#213819,#213820,#213821,#213822,#213823,#213824,#213825,#213826,#213827,
#213828,#213829,#213830,#213831,#213832,#213833,#213834,#213835,#213836,
#213837,#213838,#213839,#213840,#213841,#213842,#213843,#213844,#213845,
#213846,#213847,#213848,#213849,#213850,#213851,#213852,#213853,#213854,
#213855,#213856,#213857,#213858,#213859,#213860,#213861,#213862,#213863,
#213864,#213865,#213866,#213867,#213868,#213869,#213870,#213871,#213872,
#213873,#213874,#213875,#213876,#213877,#213878,#213879,#213880,#213881,
#213882,#213883,#213884,#213885,#213886,#213887,#213888,#213889,#213890,
#213891,#213892,#213893,#213894,#213895,#213896,#213897,#213898,#213899,
#213900,#213901,#213902,#213903,#213904,#213905,#213906,#213907,#213908,
#213909,#213910,#213911,#213912,#213913,#213914,#213915,#213916,#213917,
#213918,#213919,#213920,#213921,#213922,#213923,#213924,#213925,#213926,
#213927,#213928,#213929,#213930,#213931,#213932,#213933,#213934,#213935,
#213936,#213937,#213938,#213939,#213940,#213941,#213942,#213943,#213944,
#213945,#213946,#213947,#213948,#213949,#213950,#213951,#213952,#213953,
#213954),(#213955,#213956,#213957,#213958,#213959,#213960,#213961,#213962,
#213963,#213964,#213965,#213966,#213967,#213968,#213969,#213970,#213971,
#213972,#213973,#213974,#213975,#213976,#213977,#213978,#213979,#213980,
#213981,#213982,#213983,#213984,#213985,#213986,#213987,#213988,#213989,
#213990,#213991,#213992,#213993,#213994,#213995,#213996,#213997,#213998,
#213999,#214000,#214001,#214002,#214003,#214004,#214005,#214006,#214007,
#214008,#214009,#214010,#214011,#214012,#214013,#214014,#214015,#214016,
#214017,#214018,#214019,#214020,#214021,#214022,#214023,#214024,#214025,
#214026,#214027,#214028,#214029,#214030,#214031,#214032,#214033,#214034,
#214035,#214036,#214037,#214038,#214039,#214040,#214041,#214042,#214043,
#214044,#214045,#214046,#214047,#214048,#214049,#214050,#214051,#214052,
#214053,#214054,#214055,#214056,#214057,#214058,#214059,#214060,#214061,
#214062,#214063,#214064,#214065,#214066,#214067,#214068,#214069,#214070,
#214071,#214072,#214073,#214074,#214075,#214076,#214077,#214078,#214079,
#214080,#214081,#214082,#214083,#214084,#214085,#214086,#214087,#214088,
#214089,#214090,#214091,#214092,#214093,#214094,#214095,#214096,#214097,
#214098,#214099,#214100,#214101,#214102,#214103,#214104,#214105,#214106,
#214107,#214108,#214109,#214110,#214111,#214112,#214113,#214114,#214115,
#214116,#214117,#214118,#214119,#214120,#214121,#214122,#214123,#214124,
#214125,#214126,#214127,#214128,#214129,#214130,#214131,#214132),(#214133,
#214134,#214135,#214136,#214137,#214138,#214139,#214140,#214141,#214142,
#214143,#214144,#214145,#214146,#214147,#214148,#214149,#214150,#214151,
#214152,#214153,#214154,#214155,#214156,#214157,#214158,#214159,#214160,
#214161,#214162,#214163,#214164,#214165,#214166,#214167,#214168,#214169,
#214170,#214171,#214172,#214173,#214174,#214175,#214176,#214177,#214178,
#214179,#214180,#214181,#214182,#214183,#214184,#214185,#214186,#214187,
#214188,#214189,#214190,#214191,#214192,#214193,#214194,#214195,#214196,
#214197,#214198,#214199,#214200,#214201,#214202,#214203,#214204,#214205,
#214206,#214207,#214208,#214209,#214210,#214211,#214212,#214213,#214214,
#214215,#214216,#214217,#214218,#214219,#214220,#214221,#214222,#214223,
#214224,#214225,#214226,#214227,#214228,#214229,#214230,#214231,#214232,
#214233,#214234,#214235,#214236,#214237,#214238,#214239,#214240,#214241,
#214242,#214243,#214244,#214245,#214246,#214247,#214248,#214249,#214250,
#214251,#214252,#214253,#214254,#214255,#214256,#214257,#214258,#214259,
#214260,#214261,#214262,#214263,#214264,#214265,#214266,#214267,#214268,
#214269,#214270,#214271,#214272,#214273,#214274,#214275,#214276,#214277,
#214278,#214279,#214280,#214281,#214282,#214283,#214284,#214285,#214286,
#214287,#214288,#214289,#214290,#214291,#214292,#214293,#214294,#214295,
#214296,#214297,#214298,#214299,#214300,#214301,#214302,#214303,#214304,
#214305,#214306,#214307,#214308,#214309,#214310)),.UNSPECIFIED.,.F.,.F.,
 .F.,(4,4),(4,1,1,1,1,1,1,1,1,1,1,1,1,1,1,1,1,1,1,1,1,1,1,1,1,1,1,1,1,1,
1,1,1,1,1,1,1,1,1,1,1,1,1,1,1,1,1,1,1,1,1,1,1,1,1,1,1,1,1,1,1,1,1,1,1,1,
1,1,1,1,1,1,1,1,1,1,1,1,1,1,1,1,1,1,1,1,1,1,1,1,1,1,1,1,1,1,1,1,1,1,1,1,
1,1,1,1,1,1,1,1,1,1,1,1,1,1,1,1,1,1,1,1,1,1,1,1,1,1,1,1,1,1,1,1,1,1,1,1,
1,1,1,1,1,1,1,1,1,1,1,1,1,1,1,1,1,1,1,1,1,1,1,1,1,1,1,1,1,1,1,1,1,1,1,1,
1,4),(-0.000439583499978536,0.0515314520155978),(11.8664846510264,12.8657606844883,
13.8645971344502,14.8634335844121,15.8622700343739,16.8611064843358,17.8599429342977,
18.8587793842596,19.8576158342214,20.8564522841833,21.8552887341452,22.854125184107,
23.8529616340689,24.8517980840308,25.8506345339927,26.8494709839545,27.8483074339164,
28.8471438838783,29.8459803338402,30.844816783802,31.8436532337639,32.8424896837258,
33.8413261336877,34.8401625836495,35.8389990336114,36.8378354835733,37.8366719335352,
38.835508383497,39.8343448334589,40.8331812834208,41.8320177333827,42.8308541833445,
43.8296906333064,44.8285270832683,45.8273635332302,46.826199983192,47.8250364331539,
48.8238728831158,49.8227093330777,50.8215457830395,51.8203822330014,52.8192186829633,
53.8180551329252,54.816891582887,55.8157280328489,56.8145644828108,57.8134009327727,
58.8122373827345,59.8110738326964,60.8099102826583,61.8087467326202,62.807583182582,
63.8064196325439,64.8052560825058,65.8040925324676,66.8029289824295,67.8017654323914,
68.8006018823533,69.7994383323151,70.798274782277,71.7971112322389,72.7959476822008,
73.7947841321626,74.7936205821245,75.7924570320864,76.7912934820483,77.7901299320101,
78.788966381972,79.7878028319339,80.7866392818958,81.7854757318576,82.7843121818195,
83.7831486317814,84.7819850817433,85.7808215317051,86.779657981667,87.7784944316289,
88.7773308815908,89.7761673315526,90.7750037815145,91.7738402314764,92.7726766814383,
93.7715131314001,94.770349581362,95.7691860313239,96.7680224812858,97.7668589312476,
98.7656953812095,99.7645318311714,100.763368281133,101.762204731095,102.761041181057,
103.759877631019,104.758714080981,105.757550530943,106.756386980905,107.755223430866,
108.754059880828,109.75289633079,110.751732780752,111.750569230714,112.749405680676,
113.748242130638,114.747078580599,115.745915030561,116.744751480523,117.743587930485,
118.742424380447,119.741260830409,120.740097280371,121.738933730333,122.737770180294,
123.736606630256,124.735443080218,125.73427953018,126.733115980142,127.731952430104,
128.730788880066,129.729625330028,130.728461779989,131.727298229951,132.726134679913,
133.724971129875,134.723807579837,135.722644029799,136.721480479761,137.720316929723,
138.719153379684,139.717989829646,140.716826279608,141.71566272957,142.714499179532,
143.713335629494,144.712172079456,145.711008529418,146.709844979379,147.708681429341,
148.707517879303,149.706354329265,150.705190779227,151.704027229189,152.702863679151,
153.701700129113,154.700536579074,155.699373029036,156.698209478998,157.69704592896,
158.695882378922,159.694718828884,160.693555278846,161.692391728808,162.691228178769,
163.690064628731,164.688901078693,165.687737528655,166.686573978617,167.685410428579,
168.684246878541,169.683083328503,170.681919778464,171.680756228426,172.679592678388,
173.67842912835,174.677265578312,175.676102028274,176.674938478236,177.673774928198,
178.672611378159,179.671447828121,180.670284278083,181.669120728045,182.667957178007,
183.666793627969,184.665630077931,185.664466527893,186.663302977854),
 .UNSPECIFIED.);
#172=B_SPLINE_SURFACE_WITH_KNOTS('',3,3,((#214396,#214397,#214398,#214399,
#214400,#214401,#214402,#214403,#214404,#214405,#214406,#214407,#214408,
#214409,#214410,#214411,#214412,#214413,#214414,#214415,#214416,#214417,
#214418,#214419,#214420,#214421,#214422,#214423,#214424,#214425,#214426,
#214427,#214428,#214429,#214430,#214431,#214432,#214433,#214434,#214435,
#214436,#214437,#214438,#214439,#214440,#214441,#214442,#214443,#214444,
#214445,#214446,#214447,#214448,#214449,#214450,#214451,#214452,#214453,
#214454,#214455,#214456,#214457,#214458,#214459,#214460,#214461,#214462,
#214463,#214464,#214465,#214466,#214467,#214468,#214469,#214470,#214471,
#214472,#214473,#214474,#214475,#214476,#214477,#214478,#214479,#214480,
#214481,#214482,#214483,#214484,#214485,#214486,#214487,#214488,#214489,
#214490,#214491,#214492,#214493,#214494,#214495,#214496,#214497,#214498,
#214499,#214500,#214501,#214502,#214503,#214504,#214505,#214506,#214507,
#214508,#214509,#214510,#214511,#214512,#214513,#214514,#214515,#214516,
#214517,#214518,#214519,#214520,#214521,#214522,#214523,#214524,#214525,
#214526,#214527,#214528,#214529,#214530,#214531,#214532,#214533,#214534,
#214535,#214536,#214537,#214538,#214539,#214540,#214541,#214542,#214543,
#214544,#214545,#214546,#214547,#214548,#214549,#214550,#214551,#214552,
#214553,#214554,#214555,#214556,#214557,#214558,#214559,#214560,#214561,
#214562,#214563,#214564,#214565,#214566,#214567,#214568,#214569,#214570,
#214571,#214572,#214573),(#214574,#214575,#214576,#214577,#214578,#214579,
#214580,#214581,#214582,#214583,#214584,#214585,#214586,#214587,#214588,
#214589,#214590,#214591,#214592,#214593,#214594,#214595,#214596,#214597,
#214598,#214599,#214600,#214601,#214602,#214603,#214604,#214605,#214606,
#214607,#214608,#214609,#214610,#214611,#214612,#214613,#214614,#214615,
#214616,#214617,#214618,#214619,#214620,#214621,#214622,#214623,#214624,
#214625,#214626,#214627,#214628,#214629,#214630,#214631,#214632,#214633,
#214634,#214635,#214636,#214637,#214638,#214639,#214640,#214641,#214642,
#214643,#214644,#214645,#214646,#214647,#214648,#214649,#214650,#214651,
#214652,#214653,#214654,#214655,#214656,#214657,#214658,#214659,#214660,
#214661,#214662,#214663,#214664,#214665,#214666,#214667,#214668,#214669,
#214670,#214671,#214672,#214673,#214674,#214675,#214676,#214677,#214678,
#214679,#214680,#214681,#214682,#214683,#214684,#214685,#214686,#214687,
#214688,#214689,#214690,#214691,#214692,#214693,#214694,#214695,#214696,
#214697,#214698,#214699,#214700,#214701,#214702,#214703,#214704,#214705,
#214706,#214707,#214708,#214709,#214710,#214711,#214712,#214713,#214714,
#214715,#214716,#214717,#214718,#214719,#214720,#214721,#214722,#214723,
#214724,#214725,#214726,#214727,#214728,#214729,#214730,#214731,#214732,
#214733,#214734,#214735,#214736,#214737,#214738,#214739,#214740,#214741,
#214742,#214743,#214744,#214745,#214746,#214747,#214748,#214749,#214750,
#214751),(#214752,#214753,#214754,#214755,#214756,#214757,#214758,#214759,
#214760,#214761,#214762,#214763,#214764,#214765,#214766,#214767,#214768,
#214769,#214770,#214771,#214772,#214773,#214774,#214775,#214776,#214777,
#214778,#214779,#214780,#214781,#214782,#214783,#214784,#214785,#214786,
#214787,#214788,#214789,#214790,#214791,#214792,#214793,#214794,#214795,
#214796,#214797,#214798,#214799,#214800,#214801,#214802,#214803,#214804,
#214805,#214806,#214807,#214808,#214809,#214810,#214811,#214812,#214813,
#214814,#214815,#214816,#214817,#214818,#214819,#214820,#214821,#214822,
#214823,#214824,#214825,#214826,#214827,#214828,#214829,#214830,#214831,
#214832,#214833,#214834,#214835,#214836,#214837,#214838,#214839,#214840,
#214841,#214842,#214843,#214844,#214845,#214846,#214847,#214848,#214849,
#214850,#214851,#214852,#214853,#214854,#214855,#214856,#214857,#214858,
#214859,#214860,#214861,#214862,#214863,#214864,#214865,#214866,#214867,
#214868,#214869,#214870,#214871,#214872,#214873,#214874,#214875,#214876,
#214877,#214878,#214879,#214880,#214881,#214882,#214883,#214884,#214885,
#214886,#214887,#214888,#214889,#214890,#214891,#214892,#214893,#214894,
#214895,#214896,#214897,#214898,#214899,#214900,#214901,#214902,#214903,
#214904,#214905,#214906,#214907,#214908,#214909,#214910,#214911,#214912,
#214913,#214914,#214915,#214916,#214917,#214918,#214919,#214920,#214921,
#214922,#214923,#214924,#214925,#214926,#214927,#214928,#214929),(#214930,
#214931,#214932,#214933,#214934,#214935,#214936,#214937,#214938,#214939,
#214940,#214941,#214942,#214943,#214944,#214945,#214946,#214947,#214948,
#214949,#214950,#214951,#214952,#214953,#214954,#214955,#214956,#214957,
#214958,#214959,#214960,#214961,#214962,#214963,#214964,#214965,#214966,
#214967,#214968,#214969,#214970,#214971,#214972,#214973,#214974,#214975,
#214976,#214977,#214978,#214979,#214980,#214981,#214982,#214983,#214984,
#214985,#214986,#214987,#214988,#214989,#214990,#214991,#214992,#214993,
#214994,#214995,#214996,#214997,#214998,#214999,#215000,#215001,#215002,
#215003,#215004,#215005,#215006,#215007,#215008,#215009,#215010,#215011,
#215012,#215013,#215014,#215015,#215016,#215017,#215018,#215019,#215020,
#215021,#215022,#215023,#215024,#215025,#215026,#215027,#215028,#215029,
#215030,#215031,#215032,#215033,#215034,#215035,#215036,#215037,#215038,
#215039,#215040,#215041,#215042,#215043,#215044,#215045,#215046,#215047,
#215048,#215049,#215050,#215051,#215052,#215053,#215054,#215055,#215056,
#215057,#215058,#215059,#215060,#215061,#215062,#215063,#215064,#215065,
#215066,#215067,#215068,#215069,#215070,#215071,#215072,#215073,#215074,
#215075,#215076,#215077,#215078,#215079,#215080,#215081,#215082,#215083,
#215084,#215085,#215086,#215087,#215088,#215089,#215090,#215091,#215092,
#215093,#215094,#215095,#215096,#215097,#215098,#215099,#215100,#215101,
#215102,#215103,#215104,#215105,#215106,#215107)),.UNSPECIFIED.,.F.,.F.,
 .F.,(4,4),(4,1,1,1,1,1,1,1,1,1,1,1,1,1,1,1,1,1,1,1,1,1,1,1,1,1,1,1,1,1,
1,1,1,1,1,1,1,1,1,1,1,1,1,1,1,1,1,1,1,1,1,1,1,1,1,1,1,1,1,1,1,1,1,1,1,1,
1,1,1,1,1,1,1,1,1,1,1,1,1,1,1,1,1,1,1,1,1,1,1,1,1,1,1,1,1,1,1,1,1,1,1,1,
1,1,1,1,1,1,1,1,1,1,1,1,1,1,1,1,1,1,1,1,1,1,1,1,1,1,1,1,1,1,1,1,1,1,1,1,
1,1,1,1,1,1,1,1,1,1,1,1,1,1,1,1,1,1,1,1,1,1,1,1,1,1,1,1,1,1,1,1,1,1,1,1,
1,4),(-0.00037822144473665,0.0515928134973294),(14.3986268518925,15.3974633018543,
16.3962997518162,17.3951362017781,18.39397265174,19.3928091017018,20.3916455516637,
21.3904820016256,22.3893184515875,23.3881549015493,24.3869913515112,25.3858278014731,
26.384664251435,27.3835007013968,28.3823371513587,29.3811736013206,30.3800100512825,
31.3788465012443,32.3776829512062,33.3765194011681,34.37535585113,35.3741923010918,
36.3730287510537,37.3718652010156,38.3707016509774,39.3695381009393,40.3683745509012,
41.3672110008631,42.3660474508249,43.3648839007868,44.3637203507487,45.3625568007106,
46.3613932506724,47.3602297006343,48.3590661505962,49.3579026005581,50.3567390505199,
51.3555755004818,52.3544119504437,53.3532484004056,54.3520848503674,55.3509213003293,
56.3497577502912,57.3485942002531,58.3474306502149,59.3462671001768,60.3451035501387,
61.3439400001006,62.3427764500624,63.3416129000243,64.3404493499862,65.3392857999481,
66.3381222499099,67.3369586998718,68.3357951498337,69.3346315997956,70.3334680497574,
71.3323044997193,72.3311409496812,73.3299773996431,74.3288138496049,75.3276502995668,
76.3264867495287,77.3253231994906,78.3241596494524,79.3229960994143,80.3218325493762,
81.3206689993381,82.3195054492999,83.3183418992618,84.3171783492237,85.3160147991856,
86.3148512491474,87.3136876991093,88.3125241490712,89.3113605990331,90.3101970489949,
91.3090334989568,92.3078699489187,93.3067063988806,94.3055428488424,95.3043792988043,
96.3032157487662,97.302052198728,98.3008886486899,99.2997250986518,100.298561548614,
101.297397998576,102.296234448537,103.295070898499,104.293907348461,105.292743798423,
106.291580248385,107.290416698347,108.289253148309,109.288089598271,110.286926048232,
111.285762498194,112.284598948156,113.283435398118,114.28227184808,115.281108298042,
116.279944748004,117.278781197966,118.277617647927,119.276454097889,120.275290547851,
121.274126997813,122.272963447775,123.271799897737,124.270636347699,125.269472797661,
126.268309247622,127.267145697584,128.265982147546,129.264818597508,130.26365504747,
131.262491497432,132.261327947394,133.260164397356,134.259000847317,135.257837297279,
136.256673747241,137.255510197203,138.254346647165,139.253183097127,140.252019547089,
141.250855997051,142.249692447012,143.248528896974,144.247365346936,145.246201796898,
146.24503824686,147.243874696822,148.242711146784,149.241547596746,150.240384046707,
151.239220496669,152.238056946631,153.236893396593,154.235729846555,155.234566296517,
156.233402746479,157.232239196441,158.231075646402,159.229912096364,160.228748546326,
161.227584996288,162.22642144625,163.225257896212,164.224094346174,165.222930796136,
166.221767246097,167.220603696059,168.219440146021,169.218276595983,170.217113045945,
171.215949495907,172.214785945869,173.21362239583,174.212458845792,175.211295295754,
176.210131745716,177.208968195678,178.20780464564,179.206641095602,180.205477545564,
181.204313995525,182.203150445487,183.201986895449,184.200823345411,185.199659795373,
186.198496245335,187.197332695297,188.196169145259,189.195445174867),
 .UNSPECIFIED.);
#220=FACE_BOUND('',#5535,.T.);
#221=FACE_BOUND('',#5536,.T.);
#222=FACE_BOUND('',#5537,.T.);
#223=FACE_BOUND('',#5538,.T.);
#224=FACE_BOUND('',#5539,.T.);
#225=FACE_BOUND('',#5540,.T.);
#226=FACE_BOUND('',#5541,.T.);
#227=FACE_BOUND('',#5542,.T.);
#228=FACE_BOUND('',#5543,.T.);
#229=FACE_BOUND('',#5565,.T.);
#230=FACE_BOUND('',#5572,.T.);
#231=FACE_BOUND('',#5573,.T.);
#232=FACE_BOUND('',#5574,.T.);
#233=FACE_BOUND('',#5584,.T.);
#234=FACE_BOUND('',#5598,.T.);
#235=FACE_BOUND('',#5599,.T.);
#236=FACE_BOUND('',#5600,.T.);
#237=FACE_BOUND('',#5610,.T.);
#238=FACE_BOUND('',#5620,.T.);
#239=FACE_BOUND('',#5624,.T.);
#240=FACE_BOUND('',#5625,.T.);
#241=FACE_BOUND('',#5648,.T.);
#242=FACE_BOUND('',#5649,.T.);
#243=FACE_BOUND('',#5660,.T.);
#244=FACE_BOUND('',#5661,.T.);
#245=FACE_BOUND('',#5662,.T.);
#246=FACE_BOUND('',#5663,.T.);
#1233=B_SPLINE_CURVE_WITH_KNOTS('',3,(#128408,#128409,#128410,#128411,#128412,
#128413,#128414,#128415,#128416,#128417,#128418,#128419,#128420,#128421,
#128422,#128423,#128424,#128425,#128426,#128427,#128428,#128429,#128430,
#128431,#128432,#128433,#128434,#128435),.UNSPECIFIED.,.F.,.F.,(4,3,3,3,
3,3,3,3,3,4),(13.8747245557601,13.9615196181783,14.0483128516542,14.1350984649827,
14.2219050359775,14.2896803532321,14.3768161452291,14.4639332383284,14.5510539735215,
14.6348946358168),.UNSPECIFIED.);
#1234=B_SPLINE_CURVE_WITH_KNOTS('',3,(#128438,#128439,#128440,#128441),
 .UNSPECIFIED.,.F.,.F.,(4,4),(14.399609326548,14.6348821374693),
 .UNSPECIFIED.);
#1235=B_SPLINE_CURVE_WITH_KNOTS('',3,(#128447,#128448,#128449,#128450,#128451,
#128452,#128453,#128454,#128455,#128456,#128457,#128458,#128459,#128460,
#128461),.UNSPECIFIED.,.F.,.F.,(4,1,1,1,1,1,1,1,1,1,1,1,4),(15.707963267949,
15.7517228465151,16.2390703442761,16.7264178420371,17.2137653397981,17.7011128375591,
18.1884603353201,18.6758078330811,19.1631553308421,19.6505028286031,20.1378503263641,
20.6251978241251,20.9180878353355),.UNSPECIFIED.);
#1236=B_SPLINE_CURVE_WITH_KNOTS('',3,(#128462,#128463,#128464,#128465,#128466,
#128467,#128468,#128469,#128470,#128471,#128472,#128473,#128474,#128475,
#128476,#128477,#128478,#128479,#128480,#128481,#128482,#128483,#128484,
#128485,#128486,#128487,#128488,#128489,#128490,#128491,#128492,#128493,
#128494,#128495,#128496,#128497,#128498,#128499,#128500,#128501),
 .UNSPECIFIED.,.F.,.F.,(4,3,3,3,3,3,3,3,3,3,3,3,3,4),(14.6348946358168,
14.7220270383631,14.7770278509931,14.864154772311,14.9512651018673,15.0383784614888,
15.1254870919108,15.2126150969663,15.2643753487541,15.3512430161605,15.4404230791076,
15.5272738475405,15.6176185577448,15.707963267949),.UNSPECIFIED.);
#1237=B_SPLINE_CURVE_WITH_KNOTS('',3,(#128503,#128504,#128505,#128506,#128507,
#128508),.UNSPECIFIED.,.F.,.F.,(4,1,1,4),(14.6348821374693,14.886956824309,
15.37430432207,15.707963267949),.UNSPECIFIED.);
#1238=B_SPLINE_CURVE_WITH_KNOTS('',3,(#128509,#128510,#128511,#128512,#128513,
#128514,#128515,#128516,#128517,#128518,#128519,#128520,#128521,#128522,
#128523,#128524,#128525,#128526,#128527,#128528,#128529,#128530,#128531,
#128532,#128533,#128534,#128535,#128536,#128537,#128538,#128539,#128540,
#128541,#128542,#128543,#128544,#128545,#128546,#128547,#128548,#128549,
#128550,#128551,#128552,#128553,#128554,#128555,#128556,#128557,#128558,
#128559,#128560,#128561,#128562,#128563,#128564,#128565,#128566,#128567,
#128568,#128569,#128570,#128571,#128572,#128573,#128574,#128575,#128576,
#128577,#128578,#128579,#128580,#128581,#128582,#128583,#128584,#128585,
#128586,#128587,#128588,#128589,#128590,#128591,#128592,#128593,#128594,
#128595,#128596,#128597,#128598,#128599,#128600,#128601,#128602,#128603,
#128604,#128605,#128606,#128607,#128608,#128609,#128610,#128611,#128612,
#128613,#128614,#128615,#128616,#128617,#128618,#128619,#128620,#128621,
#128622,#128623,#128624,#128625,#128626,#128627,#128628,#128629,#128630,
#128631,#128632,#128633,#128634,#128635,#128636,#128637,#128638,#128639,
#128640,#128641,#128642,#128643,#128644,#128645,#128646,#128647,#128648,
#128649,#128650,#128651,#128652,#128653,#128654,#128655,#128656,#128657,
#128658,#128659,#128660,#128661,#128662,#128663,#128664,#128665,#128666,
#128667,#128668,#128669,#128670,#128671,#128672,#128673,#128674,#128675,
#128676,#128677,#128678,#128679,#128680,#128681,#128682,#128683,#128684,
#128685,#128686,#128687,#128688,#128689,#128690,#128691,#128692,#128693,
#128694,#128695,#128696,#128697,#128698,#128699,#128700,#128701),
 .UNSPECIFIED.,.F.,.F.,(4,3,3,3,3,3,3,3,3,3,3,3,3,3,3,3,3,3,3,3,3,3,3,3,
3,3,3,3,3,3,3,3,3,3,3,3,3,3,3,3,3,3,3,3,3,3,3,3,3,3,3,3,3,3,3,3,3,3,3,3,
3,3,3,3,4),(15.7079632709821,15.7983391757108,15.861651819831,15.9487473765214,
16.0358259589805,16.1229073061607,16.2099838502341,16.2970799349332,16.348999317592,
16.4361366999986,16.523257608915,16.6103816220701,16.6975009223997,16.7846395292193,
16.836346815353,16.923477639889,17.010591951935,17.0977093744499,17.1848221036438,
17.2719542272672,17.323694313114,17.4108212348644,17.4979315648647,17.5850449249431,
17.6721535558284,17.7592815613529,17.811041810875,17.89817343047,17.9852885340787,
18.0724067350533,18.1595202333711,18.2466531048579,18.298389308636,18.3855180458292,
18.4726302215735,18.5597454549696,18.6468559703248,18.7339858611433,18.785736806397,
18.8728666494913,18.9599799520757,19.0470963327356,19.1342080041683,19.2213390545579,
19.273084304158,19.3602139685927,19.4473270839117,19.5344432662626,19.6215547336169,
19.7086855728379,19.7604318019191,19.8475621241585,19.9346759052151,20.0217927586668,
20.1089048985344,20.1960364065272,20.2477792996801,20.334905875275,20.4220158905206,
20.5091289860856,20.5962373815784,20.6833651987953,20.7351267974411,20.8266148316514,
20.9181028658617),.UNSPECIFIED.);
#1239=B_SPLINE_CURVE_WITH_KNOTS('',3,(#128707,#128708,#128709,#128710,#128711,
#128712,#128713,#128714,#128715,#128716,#128717,#128718,#128719,#128720,
#128721,#128722,#128723,#128724,#128725,#128726,#128727,#128728,#128729,
#128730,#128731,#128732,#128733,#128734,#128735,#128736,#128737,#128738,
#128739,#128740,#128741,#128742,#128743,#128744,#128745,#128746,#128747,
#128748,#128749,#128750,#128751,#128752,#128753,#128754,#128755,#128756,
#128757,#128758,#128759,#128760,#128761,#128762,#128763,#128764,#128765,
#128766,#128767,#128768,#128769,#128770,#128771,#128772,#128773,#128774,
#128775,#128776,#128777,#128778,#128779,#128780,#128781,#128782,#128783,
#128784,#128785,#128786,#128787,#128788,#128789,#128790,#128791,#128792,
#128793,#128794,#128795,#128796,#128797,#128798,#128799,#128800,#128801,
#128802,#128803,#128804,#128805,#128806,#128807,#128808,#128809,#128810,
#128811,#128812,#128813,#128814,#128815,#128816,#128817,#128818,#128819,
#128820,#128821,#128822,#128823,#128824,#128825,#128826,#128827,#128828,
#128829,#128830,#128831,#128832,#128833,#128834,#128835,#128836,#128837,
#128838,#128839,#128840,#128841,#128842,#128843,#128844,#128845,#128846,
#128847,#128848,#128849,#128850,#128851,#128852,#128853,#128854,#128855,
#128856,#128857,#128858,#128859,#128860,#128861,#128862,#128863,#128864,
#128865,#128866,#128867,#128868,#128869,#128870,#128871,#128872,#128873,
#128874,#128875,#128876,#128877,#128878,#128879,#128880,#128881,#128882,
#128883,#128884,#128885,#128886,#128887,#128888,#128889,#128890,#128891,
#128892,#128893,#128894,#128895,#128896,#128897,#128898,#128899),
 .UNSPECIFIED.,.F.,.F.,(4,3,3,3,3,3,3,3,3,3,3,3,3,3,3,3,3,3,3,3,3,3,3,3,
3,3,3,3,3,3,3,3,3,3,3,3,3,3,3,3,3,3,3,3,3,3,3,3,3,3,3,3,3,3,3,3,3,3,3,3,
3,3,3,3,4),(21.9911485751285,22.0872403174081,22.1717043008718,22.256147550065,
22.3406073668107,22.425073290183,22.5095952809818,22.5745878151691,22.6660564577372,
22.7575140633748,22.8489170049659,22.9402589752051,23.0314877939314,23.0619353129301,
23.1465147382964,23.2310914061769,23.3157113292589,23.4003521854757,23.485071600267,
23.5492828106911,23.6336777965099,23.7180054398437,23.8022829799558,23.8865276125065,
23.9707730961945,24.0550229839529,24.1392928473558,24.2235982686224,24.3080035693484,
24.3924639475768,24.4770490018942,24.5239778062131,24.6055741796599,24.6870642443223,
24.7684687650888,24.8498084045718,24.9311114331568,25.0123964584351,25.0936820583999,
25.1749868101455,25.256382796226,25.3378246210915,25.4194048181547,25.4986728017351,
25.5832623133344,25.6677481822996,25.7521477829318,25.836478417448,25.9207557824206,
26.0050040171561,26.0892387031326,26.1734754092372,26.2577612684093,26.3420733549027,
26.426466141403,26.4733677972571,26.558092298325,26.6427552017966,26.7273710330639,
26.8119574560143,26.8965425130992,26.9607152950181,27.0519430220872,27.143293741985,
27.2010953298595),.UNSPECIFIED.);
#1240=B_SPLINE_CURVE_WITH_KNOTS('',3,(#128900,#128901,#128902,#128903,#128904,
#128905),.UNSPECIFIED.,.F.,.F.,(4,1,1,4),(20.9180878353355,21.1125453218861,
21.5998928196471,21.9911485578925),.UNSPECIFIED.);
#1241=B_SPLINE_CURVE_WITH_KNOTS('',3,(#128907,#128908,#128909,#128910,#128911,
#128912,#128913,#128914,#128915,#128916,#128917,#128918,#128919,#128920,
#128921,#128922,#128923,#128924,#128925,#128926,#128927,#128928,#128929,
#128930,#128931,#128932,#128933,#128934,#128935,#128936,#128937,#128938,
#128939,#128940,#128941,#128942,#128943,#128944,#128945,#128946,#128947,
#128948,#128949),.UNSPECIFIED.,.F.,.F.,(4,3,3,3,3,3,3,3,3,3,3,3,3,3,4),
(20.9181028658617,21.0052267765094,21.092346700924,21.1794852412345,21.2224742952021,
21.3095858066139,21.3966807230111,21.4837788139183,21.5708722938342,21.6579854628141,
21.7098217929631,21.7974543214401,21.8850676348139,21.972670334226,21.9911485751285),
 .UNSPECIFIED.);
#1242=B_SPLINE_CURVE_WITH_KNOTS('',3,(#128950,#128951,#128952,#128953,#128954,
#128955,#128956,#128957,#128958,#128959,#128960,#128961,#128962,#128963,
#128964,#128965,#128966,#128967,#128968,#128969,#128970,#128971,#128972,
#128973,#128974,#128975,#128976,#128977,#128978,#128979,#128980,#128981,
#128982,#128983,#128984,#128985,#128986,#128987,#128988,#128989,#128990,
#128991,#128992,#128993,#128994,#128995,#128996,#128997,#128998,#128999,
#129000,#129001,#129002,#129003,#129004,#129005,#129006,#129007,#129008,
#129009,#129010,#129011,#129012,#129013,#129014,#129015,#129016,#129017,
#129018,#129019,#129020,#129021,#129022,#129023,#129024,#129025,#129026,
#129027,#129028,#129029,#129030,#129031,#129032,#129033,#129034,#129035,
#129036,#129037,#129038,#129039,#129040,#129041,#129042,#129043,#129044,
#129045,#129046,#129047,#129048,#129049,#129050,#129051,#129052,#129053,
#129054,#129055,#129056,#129057,#129058,#129059,#129060,#129061,#129062,
#129063,#129064,#129065,#129066,#129067,#129068,#129069,#129070,#129071,
#129072,#129073,#129074,#129075,#129076,#129077,#129078,#129079,#129080,
#129081,#129082,#129083,#129084,#129085,#129086,#129087,#129088,#129089,
#129090,#129091,#129092,#129093,#129094,#129095,#129096,#129097,#129098,
#129099,#129100,#129101,#129102,#129103,#129104,#129105,#129106,#129107,
#129108,#129109,#129110,#129111,#129112,#129113,#129114,#129115,#129116,
#129117,#129118,#129119,#129120,#129121,#129122,#129123,#129124,#129125,
#129126,#129127,#129128,#129129,#129130,#129131,#129132,#129133,#129134,
#129135,#129136,#129137,#129138,#129139,#129140,#129141,#129142,#129143,
#129144,#129145),.UNSPECIFIED.,.F.,.F.,(4,3,3,3,3,3,3,3,3,3,3,3,3,3,3,3,
3,3,3,3,3,3,3,3,3,3,3,3,3,3,3,3,3,3,3,3,3,3,3,3,3,3,3,3,3,3,3,3,3,3,3,3,
3,3,3,3,3,3,3,3,3,3,3,3,3,4),(21.9911485753162,22.0800610136685,22.1689995435299,
22.1971692907241,22.2842690753762,22.3713523483423,22.4584390318698,22.5455212647318,
22.6326235308353,22.6845167884851,22.7716274880237,22.8587213011356,22.9458178659101,
23.0329095847879,23.1200206482753,23.1718642862461,23.2591959782146,23.3465122652369,
23.4338313118415,23.5211449598873,23.6084751333609,23.6592117840071,23.745693612034,
23.8321565252024,23.9186248608384,24.0050911555494,24.0915863725888,24.1465592817681,
24.2353201956329,24.3240706428451,24.4128143671018,24.5015423533536,24.5902572024438,
24.6339067795291,24.7183716294415,24.8028157469338,24.887276430042,24.9717432184832,
25.0562660667606,25.1212542772901,25.2127216661248,25.304178010292,25.3955797066455,
25.4869204524289,25.5781480948867,25.6086017750511,25.6931817036893,25.7777588769285,
25.8623793056185,25.9470206674601,26.0317405844674,26.0959492728121,26.1803442406884,
26.2646718670789,26.3489493912654,26.4331940089272,26.5174394793458,26.6016893548485,
26.6859592070289,26.7702646181267,26.854669910358,26.9391302810329,27.0237153293477,
27.0706442683341,27.1522360636597,27.2022275832944),.UNSPECIFIED.);
#1243=B_SPLINE_CURVE_WITH_KNOTS('',3,(#129151,#129152,#129153,#129154,#129155,
#129156,#129157,#129158,#129159,#129160,#129161,#129162,#129163,#129164,
#129165,#129166,#129167,#129168,#129169,#129170,#129171,#129172,#129173,
#129174,#129175,#129176,#129177,#129178,#129179,#129180,#129181,#129182,
#129183,#129184,#129185,#129186,#129187,#129188,#129189,#129190,#129191,
#129192,#129193,#129194,#129195,#129196,#129197,#129198,#129199,#129200,
#129201,#129202,#129203,#129204,#129205,#129206,#129207,#129208,#129209,
#129210,#129211,#129212,#129213,#129214,#129215,#129216,#129217,#129218,
#129219,#129220,#129221,#129222,#129223,#129224,#129225,#129226,#129227,
#129228,#129229,#129230,#129231,#129232,#129233,#129234,#129235,#129236,
#129237,#129238,#129239,#129240,#129241,#129242,#129243,#129244,#129245,
#129246,#129247,#129248,#129249,#129250,#129251,#129252,#129253,#129254,
#129255,#129256,#129257,#129258,#129259,#129260,#129261,#129262,#129263,
#129264,#129265,#129266,#129267,#129268,#129269,#129270,#129271,#129272,
#129273,#129274,#129275,#129276,#129277,#129278,#129279,#129280,#129281,
#129282,#129283,#129284,#129285,#129286,#129287,#129288,#129289,#129290,
#129291,#129292,#129293,#129294,#129295,#129296,#129297,#129298,#129299,
#129300,#129301,#129302,#129303,#129304,#129305,#129306,#129307,#129308,
#129309,#129310,#129311,#129312,#129313,#129314,#129315,#129316,#129317,
#129318,#129319,#129320,#129321,#129322,#129323,#129324,#129325,#129326,
#129327,#129328,#129329,#129330,#129331,#129332,#129333,#129334,#129335,
#129336,#129337,#129338,#129339,#129340,#129341,#129342,#129343,#129344,
#129345,#129346),.UNSPECIFIED.,.F.,.F.,(4,3,3,3,3,3,3,3,3,3,3,3,3,3,3,3,
3,3,3,3,3,3,3,3,3,3,3,3,3,3,3,3,3,3,3,3,3,3,3,3,3,3,3,3,3,3,3,3,3,3,3,3,
3,3,3,3,3,3,3,3,3,3,3,3,3,4),(28.2743338824266,28.3664532240664,28.4227577883011,
28.5092520935557,28.5957221727376,28.6821896165034,28.7686504765288,28.8551332349923,
28.9101052860621,28.9974342563849,29.084749014768,29.1720683332772,29.2593832734799,
29.3467162971122,29.3974527838231,29.4845626300906,29.5716559384561,29.6587525257064,
29.7458445655353,29.8329564077084,29.8848002815841,29.9719013840595,30.0589854167833,
30.1460720162916,30.233153687593,30.3202546601055,30.3721477793451,30.4593061161227,
30.5464483504257,30.6335940378146,30.7207351578585,30.8078956184438,30.8594952771061,
30.9466072614862,31.0337024468151,31.1208004982627,31.2078937641911,31.2950064517671,
31.3468427748671,31.4339808001712,31.5211023922076,31.6082271424273,31.6953472086888,
31.7824866195326,31.8341902726282,31.9213169014601,32.0084269463445,32.0955400358983,
32.1826484052062,32.2697761653463,32.3215377703892,32.4086680911823,32.4957818717525,
32.5828987261604,32.6700108677988,32.7571423788036,32.8088852681502,32.8960149192679,
32.9831280267967,33.0702442097147,33.1573556823675,33.2444865341392,33.2962327659112,
33.3833617272961,33.4704751186365,33.4844725969432),.UNSPECIFIED.);
#1244=B_SPLINE_CURVE_WITH_KNOTS('',3,(#129347,#129348,#129349,#129350,#129351,
#129352,#129353,#129354,#129355,#129356,#129357,#129358,#129359,#129360,
#129361,#129362,#129363,#129364,#129365,#129366,#129367,#129368,#129369,
#129370,#129371,#129372,#129373,#129374,#129375,#129376,#129377,#129378,
#129379,#129380,#129381,#129382,#129383,#129384,#129385,#129386),
 .UNSPECIFIED.,.F.,.F.,(4,3,3,3,3,3,3,3,3,3,3,3,3,4),(27.2010953298595,
27.2925386897041,27.3840098150324,27.4480627927791,27.532586803755,27.6170657800487,
27.7015239814603,27.7859674988434,27.8704340010683,27.9354102905401,28.0240768753705,
28.1127462609405,28.2014356078663,28.2743338823081),.UNSPECIFIED.);
#1245=B_SPLINE_CURVE_WITH_KNOTS('',3,(#129388,#129389,#129390,#129391,#129392,
#129393,#129394,#129395,#129396,#129397,#129398,#129399,#129400,#129401,
#129402,#129403,#129404,#129405,#129406,#129407,#129408,#129409,#129410,
#129411,#129412,#129413,#129414,#129415,#129416,#129417,#129418,#129419,
#129420,#129421,#129422,#129423,#129424,#129425,#129426,#129427),
 .UNSPECIFIED.,.F.,.F.,(4,3,3,3,3,3,3,3,3,3,3,3,3,4),(27.2022275832944,
27.2836626347991,27.3650248243015,27.4500641292459,27.5313531074218,27.6126363277832,
27.6939323660065,27.7752598073724,27.8566840072115,27.9381650758108,28.0197686516609,
28.0453392638561,28.1696765530861,28.2743338823081),.UNSPECIFIED.);
#1246=B_SPLINE_CURVE_WITH_KNOTS('',3,(#129428,#129429,#129430,#129431,#129432,
#129433,#129434,#129435,#129436,#129437,#129438,#129439,#129440,#129441),
 .UNSPECIFIED.,.F.,.F.,(4,1,1,1,1,1,1,1,1,1,1,4),(28.2743353147298,29.0200342593781,
29.5073817571391,29.9947292549001,30.4820767526611,30.9694242504221,31.4567717481831,
31.9441192459441,32.4314667437051,32.9188142414661,33.4061617392271,33.4844854782753),
 .UNSPECIFIED.);
#1247=B_SPLINE_CURVE_WITH_KNOTS('',3,(#129447,#129448,#129449,#129450,#129451,
#129452,#129453,#129454,#129455,#129456,#129457,#129458,#129459,#129460,
#129461,#129462,#129463,#129464,#129465,#129466,#129467,#129468,#129469,
#129470,#129471,#129472,#129473,#129474),.UNSPECIFIED.,.F.,.F.,(4,3,3,3,
3,3,3,3,3,4),(13.8747245557601,13.96151957655,14.0483127680288,14.1350983392423,
14.2219048683033,14.289680353232,14.3768161569056,14.4639332617808,14.5510540087977,
14.6348946376199),.UNSPECIFIED.);
#1248=B_SPLINE_CURVE_WITH_KNOTS('',3,(#129477,#129478,#129479,#129480),
 .UNSPECIFIED.,.F.,.F.,(4,4),(14.399609326548,14.6348821263195),
 .UNSPECIFIED.);
#1249=B_SPLINE_CURVE_WITH_KNOTS('',3,(#129486,#129487,#129488,#129489,#129490,
#129491,#129492,#129493,#129494,#129495,#129496,#129497,#129498,#129499,
#129500),.UNSPECIFIED.,.F.,.F.,(4,1,1,1,1,1,1,1,1,1,1,1,4),(15.707963267949,
15.751722846515,16.239070344276,16.7264178420371,17.2137653397981,17.7011128375591,
18.1884603353201,18.6758078330811,19.1631553308421,19.6505028286031,20.1378503263641,
20.6251978241251,20.9180878171796),.UNSPECIFIED.);
#1250=B_SPLINE_CURVE_WITH_KNOTS('',3,(#129501,#129502,#129503,#129504,#129505,
#129506,#129507,#129508,#129509,#129510,#129511,#129512,#129513,#129514,
#129515,#129516,#129517,#129518,#129519,#129520,#129521,#129522,#129523,
#129524,#129525,#129526,#129527,#129528,#129529,#129530,#129531,#129532,
#129533,#129534,#129535,#129536,#129537,#129538,#129539,#129540),
 .UNSPECIFIED.,.F.,.F.,(4,3,3,3,3,3,3,3,3,3,3,3,3,4),(14.6348946376199,
14.7220270519162,14.777027850993,14.8641547740402,14.9512651053716,15.03837846682,
15.1254870990942,15.2126151060248,15.264375348754,15.3512430123807,15.4404230762728,
15.5272738407879,15.6176185543684,15.707963267949),.UNSPECIFIED.);
#1251=B_SPLINE_CURVE_WITH_KNOTS('',3,(#129542,#129543,#129544,#129545,#129546,
#129547),.UNSPECIFIED.,.F.,.F.,(4,1,1,4),(14.6348821263195,14.886956824309,
15.37430432207,15.707963267949),.UNSPECIFIED.);
#1252=B_SPLINE_CURVE_WITH_KNOTS('',3,(#129548,#129549,#129550,#129551,#129552,
#129553,#129554,#129555,#129556,#129557,#129558,#129559,#129560,#129561,
#129562,#129563,#129564,#129565,#129566,#129567,#129568,#129569,#129570,
#129571,#129572,#129573,#129574,#129575,#129576,#129577,#129578,#129579,
#129580,#129581,#129582,#129583,#129584,#129585,#129586,#129587,#129588,
#129589,#129590,#129591,#129592,#129593,#129594,#129595,#129596,#129597,
#129598,#129599,#129600,#129601,#129602,#129603,#129604,#129605,#129606,
#129607,#129608,#129609,#129610,#129611,#129612,#129613,#129614,#129615,
#129616,#129617,#129618,#129619,#129620,#129621,#129622,#129623,#129624,
#129625,#129626,#129627,#129628,#129629,#129630,#129631,#129632,#129633,
#129634,#129635,#129636,#129637,#129638,#129639,#129640,#129641,#129642,
#129643,#129644,#129645,#129646,#129647,#129648,#129649,#129650,#129651,
#129652,#129653,#129654,#129655,#129656,#129657,#129658,#129659,#129660,
#129661,#129662,#129663,#129664,#129665,#129666,#129667,#129668,#129669,
#129670,#129671,#129672,#129673,#129674,#129675,#129676,#129677,#129678,
#129679,#129680,#129681,#129682,#129683,#129684,#129685,#129686,#129687,
#129688,#129689,#129690,#129691,#129692,#129693,#129694,#129695,#129696,
#129697,#129698,#129699,#129700,#129701,#129702,#129703,#129704,#129705,
#129706,#129707,#129708,#129709,#129710,#129711,#129712,#129713,#129714,
#129715,#129716,#129717,#129718,#129719,#129720,#129721,#129722,#129723,
#129724,#129725,#129726,#129727,#129728,#129729,#129730,#129731,#129732,
#129733,#129734,#129735,#129736,#129737,#129738,#129739,#129740),
 .UNSPECIFIED.,.F.,.F.,(4,3,3,3,3,3,3,3,3,3,3,3,3,3,3,3,3,3,3,3,3,3,3,3,
3,3,3,3,3,3,3,3,3,3,3,3,3,3,3,3,3,3,3,3,3,3,3,3,3,3,3,3,3,3,3,3,3,3,3,3,
3,3,3,3,4),(15.7079632709815,15.7983388023486,15.861651819831,15.9487475083028,
16.0358262241585,16.122907705879,16.2099843848246,16.2970806037435,16.348999317592,
16.4361366409196,16.5232574899998,16.6103814427677,16.6975006825434,16.784639229082,
16.836346815353,16.9234776545726,17.010591981452,17.0977094188805,17.1848221629971,
17.2719543014269,17.323694313114,17.4108212370465,17.4979315692867,17.5850449316705,
17.6721535648929,17.7592815727834,17.811041810875,17.898173425061,17.9852885231696,
18.0724067185609,18.1595202112614,18.2466530771275,18.298389308636,18.3855180493059,
18.4726302285909,18.559745465589,18.6468559845724,18.7339858790278,18.785736806397,
18.8728666485425,18.959979950145,19.0470963297829,19.1342080001734,19.2213390494988,
19.273084304158,19.3602139689286,19.4473270846037,19.534443267337,19.6215547350878,
19.7086855747234,19.760431801919,19.8475621199502,19.9346758967653,20.0217927459667,
20.1089048815892,20.1960363853822,20.24777929968,20.3349058916832,20.4220159234169,
20.5091290354302,20.5962374473095,20.6833652806739,20.735126797441,20.8266148322207,
20.9181028670005),.UNSPECIFIED.);
#1253=B_SPLINE_CURVE_WITH_KNOTS('',3,(#129746,#129747,#129748,#129749,#129750,
#129751,#129752,#129753,#129754,#129755,#129756,#129757,#129758,#129759,
#129760,#129761,#129762,#129763,#129764,#129765,#129766,#129767,#129768,
#129769,#129770,#129771,#129772,#129773,#129774,#129775,#129776,#129777,
#129778,#129779,#129780,#129781,#129782,#129783,#129784,#129785,#129786,
#129787,#129788,#129789,#129790,#129791,#129792,#129793,#129794,#129795,
#129796,#129797,#129798,#129799,#129800,#129801,#129802,#129803,#129804,
#129805,#129806,#129807,#129808,#129809,#129810,#129811,#129812,#129813,
#129814,#129815,#129816,#129817,#129818,#129819,#129820,#129821,#129822,
#129823,#129824,#129825,#129826,#129827,#129828,#129829,#129830,#129831,
#129832,#129833,#129834,#129835,#129836,#129837,#129838,#129839,#129840,
#129841,#129842,#129843,#129844,#129845,#129846,#129847,#129848,#129849,
#129850,#129851,#129852,#129853,#129854,#129855,#129856,#129857,#129858,
#129859,#129860,#129861,#129862,#129863,#129864,#129865,#129866,#129867,
#129868,#129869,#129870,#129871,#129872,#129873,#129874,#129875,#129876,
#129877,#129878,#129879,#129880,#129881,#129882,#129883,#129884,#129885,
#129886,#129887,#129888,#129889,#129890,#129891,#129892,#129893,#129894,
#129895,#129896,#129897,#129898,#129899,#129900,#129901,#129902,#129903,
#129904,#129905,#129906,#129907,#129908,#129909,#129910,#129911,#129912,
#129913,#129914,#129915,#129916,#129917,#129918,#129919,#129920,#129921,
#129922,#129923,#129924,#129925,#129926,#129927,#129928,#129929,#129930,
#129931,#129932,#129933,#129934,#129935,#129936,#129937,#129938),
 .UNSPECIFIED.,.F.,.F.,(4,3,3,3,3,3,3,3,3,3,3,3,3,3,3,3,3,3,3,3,3,3,3,3,
3,3,3,3,3,3,3,3,3,3,3,3,3,3,3,3,3,3,3,3,3,3,3,3,3,3,3,3,3,3,3,3,3,3,3,3,
3,3,3,3,4),(21.9911485751285,22.0872403174081,22.1717077643695,22.2561544844513,
22.3406177643316,22.4250871456575,22.5096125640496,22.5745878151691,22.6660514455681,
22.7575040081467,22.8489019715955,22.9402390467649,23.0314631630385,23.0619353129301,
23.1465167513392,23.2310954406082,23.3157173860693,23.4003602647288,23.4850816883209,
23.5492828106911,23.6336777241022,23.718005299017,23.8022827747739,23.8865273471115,
23.9707727770584,24.0550226151273,24.1392924329723,24.2235978128946,24.3080030789759,
24.392463426326,24.4770484559771,24.5239778062131,24.605573799559,24.687063482264,
24.768467619494,24.8498068741233,24.9311095168766,25.0123941556193,25.0936793685603,
25.1749837330107,25.2563793332897,25.337820772415,25.419400587678,25.4986728017351,
25.583262289203,25.6677481290383,25.7521476956501,25.8364782913607,25.9207556105826,
26.0050037953159,26.0892384271216,26.1734750749651,26.2577608699837,26.3420728889482,
26.4264656031797,26.4733677972571,26.5580943048163,26.642759224378,26.727377075819,
26.811965520082,26.8965525888318,26.9607152950181,27.0519383065955,27.1432841150039,
27.2010954696436),.UNSPECIFIED.);
#1254=B_SPLINE_CURVE_WITH_KNOTS('',3,(#129939,#129940,#129941,#129942,#129943,
#129944),.UNSPECIFIED.,.F.,.F.,(4,1,1,4),(20.9180878171796,21.1125453218861,
21.5998928196471,21.991148557883),.UNSPECIFIED.);
#1255=B_SPLINE_CURVE_WITH_KNOTS('',3,(#129946,#129947,#129948,#129949,#129950,
#129951,#129952,#129953,#129954,#129955,#129956,#129957,#129958,#129959,
#129960,#129961,#129962,#129963,#129964,#129965,#129966,#129967,#129968,
#129969,#129970,#129971,#129972,#129973,#129974,#129975,#129976,#129977,
#129978,#129979,#129980,#129981,#129982,#129983,#129984,#129985,#129986,
#129987,#129988),.UNSPECIFIED.,.F.,.F.,(4,3,3,3,3,3,3,3,3,3,3,3,3,3,4),
(20.9181028670005,21.0052267362147,21.0923466194079,21.179485119142,21.222474295202,
21.3095858862927,21.3966808826214,21.4837790530665,21.5708726121089,21.6579858588928,
21.709821792963,21.797454164746,21.8850673211435,21.9726698643262,21.9911485751285),
 .UNSPECIFIED.);
#1256=B_SPLINE_CURVE_WITH_KNOTS('',3,(#129989,#129990,#129991,#129992,#129993,
#129994,#129995,#129996,#129997,#129998,#129999,#130000,#130001,#130002,
#130003,#130004,#130005,#130006,#130007,#130008,#130009,#130010,#130011,
#130012,#130013,#130014,#130015,#130016,#130017,#130018,#130019,#130020,
#130021,#130022,#130023,#130024,#130025,#130026,#130027,#130028,#130029,
#130030,#130031,#130032,#130033,#130034,#130035,#130036,#130037,#130038,
#130039,#130040,#130041,#130042,#130043,#130044,#130045,#130046,#130047,
#130048,#130049,#130050,#130051,#130052,#130053,#130054,#130055,#130056,
#130057,#130058,#130059,#130060,#130061,#130062,#130063,#130064,#130065,
#130066,#130067,#130068,#130069,#130070,#130071,#130072,#130073,#130074,
#130075,#130076,#130077,#130078,#130079,#130080,#130081,#130082,#130083,
#130084,#130085,#130086,#130087,#130088,#130089,#130090,#130091,#130092,
#130093,#130094,#130095,#130096,#130097,#130098,#130099,#130100,#130101,
#130102,#130103,#130104,#130105,#130106,#130107,#130108,#130109,#130110,
#130111,#130112,#130113,#130114,#130115,#130116,#130117,#130118,#130119,
#130120,#130121,#130122,#130123,#130124,#130125,#130126,#130127,#130128,
#130129,#130130,#130131,#130132,#130133,#130134,#130135,#130136,#130137,
#130138,#130139,#130140,#130141,#130142,#130143,#130144,#130145,#130146,
#130147,#130148,#130149,#130150,#130151,#130152,#130153,#130154,#130155,
#130156,#130157,#130158,#130159,#130160,#130161,#130162,#130163,#130164,
#130165,#130166,#130167,#130168,#130169,#130170,#130171,#130172,#130173,
#130174,#130175,#130176,#130177,#130178,#130179,#130180,#130181,#130182,
#130183,#130184),.UNSPECIFIED.,.F.,.F.,(4,3,3,3,3,3,3,3,3,3,3,3,3,3,3,3,
3,3,3,3,3,3,3,3,3,3,3,3,3,3,3,3,3,3,3,3,3,3,3,3,3,3,3,3,3,3,3,3,3,3,3,3,
3,3,3,3,3,3,3,3,3,3,3,3,3,4),(21.9911485753162,22.0800609495919,22.168999417996,
22.1971692907241,22.2842691742849,22.3713525460866,22.4584393273926,22.5455216572055,
22.6326240181457,22.6845167884851,22.7716275763734,22.8587214790213,22.9458181342347,
23.0329099438452,23.120021097721,23.1718642862461,23.2591953323291,23.3465109695105,
23.4338293669418,23.5211423678883,23.60847190326,23.6592117840071,23.7456953098164,
23.832159927636,23.9186299638456,24.005097953844,24.0915948443439,24.1465592817681,
24.2353164039209,24.3240630384395,24.4128029701689,24.5015271920606,24.5902383597612,
24.6339067795291,24.7183759992437,24.8028244958566,24.8872895482853,24.9717606994971,
25.0562878722159,25.1212542772901,25.212715341686,25.3041653224886,25.3955607374181,
25.486895306588,25.578117015447,25.6086017750511,25.6931842451492,25.7777639703814,
25.8623869523081,25.9470308674618,26.0317533205491,26.0959492728121,26.1803441484525,
26.2646716876325,26.3489491297302,26.433193670525,26.5174390722406,26.6016888841523,
26.6859586779554,26.770264035995,26.8546692836303,26.9391296144661,27.0237146307952,
27.0706442683341,27.1522355848392,27.2022276034959),.UNSPECIFIED.);
#1257=B_SPLINE_CURVE_WITH_KNOTS('',3,(#130190,#130191,#130192,#130193,#130194,
#130195,#130196,#130197,#130198,#130199,#130200,#130201,#130202,#130203,
#130204,#130205,#130206,#130207,#130208,#130209,#130210,#130211,#130212,
#130213,#130214,#130215,#130216,#130217,#130218,#130219,#130220,#130221,
#130222,#130223,#130224,#130225,#130226,#130227,#130228,#130229,#130230,
#130231,#130232,#130233,#130234,#130235,#130236,#130237,#130238,#130239,
#130240,#130241,#130242,#130243,#130244,#130245,#130246,#130247,#130248,
#130249,#130250,#130251,#130252,#130253,#130254,#130255,#130256,#130257,
#130258,#130259,#130260,#130261,#130262,#130263,#130264,#130265,#130266,
#130267,#130268,#130269,#130270,#130271,#130272,#130273,#130274,#130275,
#130276,#130277,#130278,#130279,#130280,#130281,#130282,#130283,#130284,
#130285,#130286,#130287,#130288,#130289,#130290,#130291,#130292,#130293,
#130294,#130295,#130296,#130297,#130298,#130299,#130300,#130301,#130302,
#130303,#130304,#130305,#130306,#130307,#130308,#130309,#130310,#130311,
#130312,#130313,#130314,#130315,#130316,#130317,#130318,#130319,#130320,
#130321,#130322,#130323,#130324,#130325,#130326,#130327,#130328,#130329,
#130330,#130331,#130332,#130333,#130334,#130335,#130336,#130337,#130338,
#130339,#130340,#130341,#130342,#130343,#130344,#130345,#130346,#130347,
#130348,#130349,#130350,#130351,#130352,#130353,#130354,#130355,#130356,
#130357,#130358,#130359,#130360,#130361,#130362,#130363,#130364,#130365,
#130366,#130367,#130368,#130369,#130370,#130371,#130372,#130373,#130374,
#130375,#130376,#130377,#130378,#130379,#130380,#130381,#130382,#130383,
#130384,#130385),.UNSPECIFIED.,.F.,.F.,(4,3,3,3,3,3,3,3,3,3,3,3,3,3,3,3,
3,3,3,3,3,3,3,3,3,3,3,3,3,3,3,3,3,3,3,3,3,3,3,3,3,3,3,3,3,3,3,3,3,3,3,3,
3,3,3,3,3,3,3,3,3,3,3,3,3,4),(28.2743338824266,28.3664499676938,28.4227577883011,
28.5092534192787,28.5957248380328,28.6821936309558,28.768655843137,28.8551399477051,
28.9101052860621,28.9974337506621,29.0847479974582,29.1720668007956,29.2593812251369,
29.3467137364858,29.3974527838231,29.4845627017913,29.5716560821199,29.658752741023,
29.7458448521569,29.8329567644714,29.8848002815841,29.9719014591824,30.0589855683635,
30.1460722455977,30.2331539951607,30.3202550460865,30.3721477793451,30.4593060263713,
30.5464481695862,30.6335937647714,30.7207347922023,30.8078951603531,30.8594952771061,
30.9466073231606,31.0337025710101,31.1208006856437,31.2078940149848,31.2950067657722,
31.3468427748671,31.4339807679861,31.5211023274172,31.6082270447182,31.6953470779628,
31.7824864559265,31.8341902726281,31.9213169142658,32.0084269721101,32.0955400747291,
32.1826484571305,32.2697762302935,32.3215377703891,32.4086680878499,32.4957818650579,
32.5828987160914,32.6700108543567,32.75714236202,32.8088852681501,32.8960149195982,
32.9831280274467,33.0702442106651,33.1573556836068,33.2444865356467,33.2962327659111,
33.3833617264479,33.4704751169556,33.4844725988534),.UNSPECIFIED.);
#1258=B_SPLINE_CURVE_WITH_KNOTS('',3,(#130386,#130387,#130388,#130389,#130390,
#130391,#130392,#130393,#130394,#130395,#130396,#130397,#130398,#130399,
#130400,#130401,#130402,#130403,#130404,#130405,#130406,#130407,#130408,
#130409,#130410,#130411,#130412,#130413,#130414,#130415,#130416,#130417,
#130418,#130419,#130420,#130421,#130422,#130423,#130424,#130425),
 .UNSPECIFIED.,.F.,.F.,(4,3,3,3,3,3,3,3,3,3,3,3,3,4),(27.2010954696436,
27.2925337945715,27.3839999022843,27.4480627927791,27.5325902280114,27.617072650843,
27.7015343147517,27.7859813021922,27.8704512660146,27.9354102905401,28.0240739238239,
28.1127403128143,28.2014266288529,28.2743338823081),.UNSPECIFIED.);
#1259=B_SPLINE_CURVE_WITH_KNOTS('',3,(#130427,#130428,#130429,#130430,#130431,
#130432,#130433,#130434,#130435,#130436,#130437,#130438,#130439,#130440,
#130441,#130442,#130443,#130444,#130445,#130446,#130447,#130448,#130449,
#130450,#130451,#130452,#130453,#130454,#130455,#130456,#130457,#130458,
#130459,#130460,#130461,#130462,#130463,#130464,#130465,#130466),
 .UNSPECIFIED.,.F.,.F.,(4,3,3,3,3,3,3,3,3,3,3,3,3,4),(27.2022276034959,
27.2836621718988,27.3650238767157,27.4500633001082,27.5313517914947,27.6126345246834,
27.6939300756229,27.7752570298697,27.8566807447005,27.9381613288421,28.0197644242444,
28.0453392638561,28.1696867713369,28.2743338823081),.UNSPECIFIED.);
#1260=B_SPLINE_CURVE_WITH_KNOTS('',3,(#130467,#130468,#130469,#130470,#130471,
#130472,#130473,#130474,#130475,#130476,#130477,#130478,#130479,#130480),
 .UNSPECIFIED.,.F.,.F.,(4,1,1,1,1,1,1,1,1,1,1,4),(28.2743353127056,29.0200342593781,
29.5073817571391,29.9947292549001,30.4820767526611,30.9694242504221,31.4567717481831,
31.9441192459441,32.4314667437051,32.9188142414661,33.4061617392271,33.4844854751707),
 .UNSPECIFIED.);
#1261=B_SPLINE_CURVE_WITH_KNOTS('',3,(#130486,#130487,#130488,#130489,#130490,
#130491,#130492,#130493),.UNSPECIFIED.,.F.,.F.,(4,1,1,1,1,4),(15.707963267949,
15.8622700343739,16.8611064843358,17.8599429342977,18.8587793842595,19.7647623348627),
 .UNSPECIFIED.);
#1262=B_SPLINE_CURVE_WITH_KNOTS('',3,(#130495,#130496,#130497,#130498,#130499,
#130500,#130501,#130502,#130503,#130504,#130505,#130506,#130507,#130508,
#130509,#130510,#130511,#130512,#130513,#130514,#130515,#130516,#130517,
#130518,#130519,#130520,#130521,#130522,#130523,#130524,#130525,#130526,
#130527,#130528,#130529,#130530,#130531,#130532,#130533,#130534,#130535,
#130536,#130537,#130538,#130539,#130540,#130541,#130542,#130543,#130544,
#130545,#130546,#130547,#130548,#130549,#130550,#130551,#130552),
 .UNSPECIFIED.,.F.,.F.,(4,3,3,3,3,3,3,3,3,3,3,3,3,3,3,3,3,3,3,4),(13.8757070305574,
13.9742332816752,14.0726192270832,14.1714710217493,14.269679438043,14.3678547454402,
14.4660265209369,14.5653782868057,14.6636879754741,14.7635607799431,14.8634335844121,
14.9606976685948,15.0578044132827,15.154822913635,15.2517842191042,15.3487193065272,
15.4457083690103,15.5427241666821,15.6398692546785,15.707963267949),
 .UNSPECIFIED.);
#1263=B_SPLINE_CURVE_WITH_KNOTS('',3,(#130556,#130557,#130558,#130559,#130560),
 .UNSPECIFIED.,.F.,.F.,(4,1,4),(14.3986268518925,15.3974633018543,15.707963267949),
 .UNSPECIFIED.);
#1264=B_SPLINE_CURVE_WITH_KNOTS('',3,(#130561,#130562,#130563,#130564,#130565,
#130566,#130567,#130568),.UNSPECIFIED.,.F.,.F.,(4,1,1,1,1,4),(15.707963267949,
16.3962997518162,17.3951362017781,18.39397265174,19.3928091017018,19.7659327733658),
 .UNSPECIFIED.);
#1265=B_SPLINE_CURVE_WITH_KNOTS('',3,(#130574,#130575,#130576,#130577,#130578,
#130579,#130580,#130581),.UNSPECIFIED.,.F.,.F.,(4,1,1,1,1,4),(21.9911485751286,
22.854125184107,23.8529616340689,24.8517980840308,25.8506345339927,26.0493850673138),
 .UNSPECIFIED.);
#1266=B_SPLINE_CURVE_WITH_KNOTS('',3,(#130582,#130583,#130584,#130585,#130586,
#130587,#130588),.UNSPECIFIED.,.F.,.F.,(4,1,1,1,4),(19.7647623348627,19.8576158342214,
20.8564522841833,21.8552887341452,21.9911485751286),.UNSPECIFIED.);
#1267=B_SPLINE_CURVE_WITH_KNOTS('',3,(#130590,#130591,#130592,#130593,#130594,
#130595),.UNSPECIFIED.,.F.,.F.,(4,1,1,4),(19.7659327733658,20.3916455516637,
21.3904820016256,21.9911485751286),.UNSPECIFIED.);
#1268=B_SPLINE_CURVE_WITH_KNOTS('',3,(#130596,#130597,#130598,#130599,#130600,
#130601,#130602,#130603,#130604,#130605,#130606,#130607,#130608,#130609,
#130610,#130611,#130612,#130613,#130614,#130615,#130616,#130617,#130618,
#130619,#130620,#130621,#130622,#130623,#130624,#130625,#130626,#130627,
#130628,#130629,#130630,#130631,#130632,#130633,#130634,#130635,#130636,
#130637,#130638,#130639,#130640,#130641,#130642,#130643,#130644,#130645,
#130646,#130647,#130648,#130649,#130650,#130651,#130652,#130653,#130654,
#130655,#130656,#130657,#130658,#130659,#130660,#130661,#130662,#130663,
#130664,#130665,#130666,#130667,#130668,#130669,#130670,#130671,#130672,
#130673,#130674,#130675,#130676,#130677,#130678,#130679,#130680,#130681,
#130682,#130683,#130684,#130685,#130686,#130687,#130688,#130689,#130690,
#130691,#130692,#130693,#130694,#130695,#130696,#130697,#130698,#130699,
#130700,#130701,#130702,#130703,#130704,#130705,#130706,#130707,#130708,
#130709,#130710,#130711,#130712,#130713,#130714,#130715,#130716,#130717,
#130718,#130719),.UNSPECIFIED.,.F.,.F.,(4,3,3,3,3,3,3,3,3,3,3,3,3,3,3,3,
3,3,3,3,3,3,3,3,3,3,3,3,3,3,3,3,3,3,3,3,3,3,3,3,3,4),(21.9911487995834,
22.0999040669592,22.2090426071739,22.318716159435,22.3893184515875,22.4879213274736,
22.5863838945598,22.6866052704335,22.7848896590421,22.8831410757094,22.9813889965946,
23.0830804728333,23.1814696748722,23.2848122882107,23.3881549015493,23.486755194993,
23.585215198191,23.685437217356,23.7837191074787,23.8819680557453,23.9802135417613,
24.0819079941988,24.1802948708398,24.2836431111755,24.3869913515112,24.4855869791747,
24.584042226434,24.6842654233139,24.7825423701227,24.8807863158073,24.9790267464169,
25.0807270101809,25.1791087505825,25.2824682760278,25.3858278014731,25.4844081043906,
25.5828572791635,25.6812050451075,25.7794880184323,25.8777310276212,25.9759959080335,
26.0480412283342),.UNSPECIFIED.);
#1269=B_SPLINE_CURVE_WITH_KNOTS('',3,(#130725,#130726,#130727,#130728,#130729,
#130730,#130731,#130732,#130733,#130734,#130735,#130736,#130737,#130738,
#130739,#130740,#130741,#130742,#130743,#130744,#130745,#130746,#130747,
#130748,#130749,#130750,#130751,#130752,#130753,#130754,#130755,#130756,
#130757,#130758,#130759,#130760,#130761,#130762,#130763,#130764,#130765,
#130766,#130767,#130768,#130769,#130770,#130771,#130772,#130773,#130774,
#130775,#130776,#130777,#130778,#130779,#130780,#130781,#130782,#130783,
#130784,#130785,#130786,#130787,#130788,#130789,#130790,#130791,#130792,
#130793,#130794,#130795,#130796,#130797,#130798,#130799,#130800,#130801,
#130802,#130803,#130804,#130805,#130806,#130807,#130808,#130809,#130810,
#130811,#130812,#130813,#130814,#130815,#130816,#130817,#130818,#130819,
#130820,#130821,#130822,#130823,#130824,#130825,#130826,#130827,#130828,
#130829,#130830,#130831,#130832,#130833,#130834,#130835,#130836,#130837,
#130838,#130839,#130840,#130841,#130842,#130843,#130844,#130845,#130846,
#130847,#130848),.UNSPECIFIED.,.F.,.F.,(4,3,3,3,3,3,3,3,3,3,3,3,3,3,3,3,
3,3,3,3,3,3,3,3,3,3,3,3,3,3,3,3,3,3,3,3,3,3,3,3,3,4),(28.2743338823082,
28.3746245108422,28.4749734042942,28.5754886326583,28.6760922711292,28.7769068634701,
28.8471438838783,28.9457420298706,29.0441998338806,29.1444223963755,29.2427019757815,
29.3409485766512,29.4391916815761,29.5408888446421,29.6392732799478,29.742626806894,
29.8459803338402,29.9445784592305,30.0430362424602,30.1432588101279,30.2415383684702,
30.3397849482168,30.4380280319867,30.5397252199405,30.6381096342302,30.7414632090161,
30.844816783802,30.9434149029363,31.0418726797403,31.1420952489933,31.2403748005386,
31.3386213733642,31.4368644500979,31.5385616460144,31.6369460530499,31.7402996434069,
31.8436532337639,31.9422528703022,32.0406907036442,32.139033758075,32.2373181769404,
32.3317147877909),.UNSPECIFIED.);
#1270=B_SPLINE_CURVE_WITH_KNOTS('',3,(#130849,#130850,#130851,#130852,#130853,
#130854),.UNSPECIFIED.,.F.,.F.,(4,1,1,4),(26.0493850673138,26.8494709839545,
27.8483074339164,28.2743284150372),.UNSPECIFIED.);
#1271=B_SPLINE_CURVE_WITH_KNOTS('',3,(#130856,#130857,#130858,#130859,#130860,
#130861,#130862,#130863,#130864,#130865,#130866,#130867,#130868,#130869,
#130870,#130871,#130872,#130873,#130874,#130875,#130876,#130877,#130878,
#130879,#130880,#130881,#130882,#130883,#130884,#130885,#130886,#130887,
#130888,#130889,#130890,#130891,#130892,#130893,#130894,#130895,#130896,
#130897,#130898,#130899,#130900,#130901,#130902,#130903,#130904,#130905,
#130906,#130907,#130908,#130909,#130910,#130911,#130912,#130913,#130914,
#130915,#130916,#130917,#130918,#130919,#130920,#130921,#130922,#130923,
#130924,#130925,#130926,#130927,#130928),.UNSPECIFIED.,.F.,.F.,(4,3,3,3,
3,3,3,3,3,3,3,3,3,3,3,3,3,3,3,3,3,3,3,3,4),(26.0480412283342,26.1464094056132,
26.2448398400683,26.3434312868597,26.3846642514349,26.4832625888546,26.5817205901414,
26.6819431040484,26.7802228937311,26.8784697092845,26.9767130330315,27.0784099501228,
27.1767946124098,27.2801476569033,27.3835007013968,27.4808124354761,27.5800026163015,
27.6770619119092,27.7740624145151,27.8710350582304,27.9718597641926,28.0689211628773,
28.1660361043295,28.2632831523914,28.2743338820794),.UNSPECIFIED.);
#1272=B_SPLINE_CURVE_WITH_KNOTS('',3,(#130929,#130930,#130931,#130932,#130933,
#130934,#130935,#130936,#130937,#130938,#130939,#130940,#130941,#130942,
#130943,#130944,#130945,#130946,#130947,#130948,#130949,#130950,#130951,
#130952,#130953,#130954,#130955,#130956,#130957,#130958,#130959,#130960,
#130961,#130962,#130963,#130964,#130965,#130966,#130967,#130968,#130969,
#130970,#130971,#130972,#130973,#130974,#130975,#130976,#130977,#130978,
#130979,#130980,#130981,#130982,#130983,#130984,#130985,#130986,#130987,
#130988,#130989,#130990,#130991,#130992,#130993,#130994,#130995,#130996,
#130997,#130998,#130999,#131000,#131001,#131002,#131003,#131004,#131005,
#131006,#131007,#131008,#131009,#131010,#131011,#131012,#131013,#131014,
#131015,#131016,#131017,#131018,#131019,#131020,#131021,#131022,#131023,
#131024,#131025,#131026,#131027,#131028,#131029,#131030,#131031,#131032,
#131033,#131034,#131035,#131036,#131037,#131038,#131039,#131040,#131041,
#131042,#131043,#131044,#131045,#131046,#131047,#131048,#131049,#131050,
#131051,#131052),.UNSPECIFIED.,.F.,.F.,(4,3,3,3,3,3,3,3,3,3,3,3,3,3,3,3,
3,3,3,3,3,3,3,3,3,3,3,3,3,3,3,3,3,3,3,3,3,3,3,3,3,4),(28.2743338823082,
28.3823371513587,28.4809354101241,28.5793933280734,28.6796158622293,28.7778955576022,
28.8761422749412,28.9743854966836,29.0760825228428,29.1744670746393,29.27782033798,
29.3811736013206,29.4797717427214,29.5782295425657,29.6784521061552,29.7767316824828,
29.8749782806886,29.9732213833692,30.0749185503475,30.1733029844888,30.2766565178856,
30.3800100512824,30.4786081310516,30.5770658678374,30.6772884470132,30.775567957224,
30.8738144883134,30.9720575229635,31.0737547675337,31.1721391320451,31.2754928166447,
31.3788465012443,31.4774477473609,31.5759078066966,31.6742504131636,31.7725287580314,
31.8707723649811,31.969010716645,32.0673303011073,32.165692245105,32.2642027660236,
32.3314303398525),.UNSPECIFIED.);
#1273=B_SPLINE_CURVE_WITH_KNOTS('',3,(#131058,#131059,#131060,#131061,#131062,
#131063,#131064,#131065,#131066,#131067,#131068,#131069,#131070,#131071,
#131072,#131073,#131074,#131075,#131076,#131077,#131078,#131079,#131080,
#131081,#131082,#131083,#131084,#131085,#131086,#131087,#131088,#131089,
#131090,#131091,#131092,#131093,#131094,#131095,#131096,#131097,#131098,
#131099,#131100,#131101,#131102,#131103,#131104,#131105,#131106,#131107,
#131108,#131109,#131110,#131111,#131112,#131113,#131114,#131115,#131116,
#131117,#131118,#131119,#131120,#131121,#131122,#131123,#131124,#131125,
#131126,#131127,#131128,#131129,#131130,#131131,#131132,#131133,#131134,
#131135,#131136,#131137,#131138,#131139,#131140,#131141,#131142,#131143,
#131144,#131145,#131146,#131147,#131148,#131149,#131150,#131151,#131152,
#131153,#131154,#131155,#131156,#131157,#131158,#131159,#131160,#131161,
#131162,#131163,#131164,#131165,#131166,#131167,#131168,#131169,#131170,
#131171,#131172,#131173,#131174,#131175,#131176,#131177,#131178,#131179,
#131180,#131181),.UNSPECIFIED.,.F.,.F.,(4,3,3,3,3,3,3,3,3,3,3,3,3,3,3,3,
3,3,3,3,3,3,3,3,3,3,3,3,3,3,3,3,3,3,3,3,3,3,3,3,3,4),(34.5575191897594,
34.6782345503758,34.8009387396348,34.8401625836495,34.9387607091264,35.0372184923827,
35.1374410600363,35.2357206182558,35.3339671978241,35.4322102813602,35.533907469423,
35.6322918833412,35.7356454584763,35.8389990336114,35.9375971585486,36.036054941259,
36.1362775090483,36.234557066711,36.3328036457193,36.4310467286934,36.5327439174134,
36.6311283307699,36.7344819071716,36.8378354835733,36.9364336084869,37.0348913911719,
37.1351139589673,37.2333935165999,37.3316400955765,37.4298831785171,37.5315803672716,
37.629964780591,37.7333183570631,37.8366719335352,37.9352415778354,38.0336830992399,
38.1320262040974,38.2303004962056,38.3285627936512,38.4268127465159,38.5251372404659,
38.6142676516065),.UNSPECIFIED.);
#1274=B_SPLINE_CURVE_WITH_KNOTS('',3,(#131182,#131183,#131184,#131185,#131186,
#131187,#131188,#131189,#131190,#131191,#131192,#131193,#131194,#131195,
#131196,#131197,#131198,#131199,#131200,#131201,#131202,#131203,#131204,
#131205,#131206,#131207,#131208,#131209,#131210,#131211,#131212,#131213,
#131214,#131215,#131216,#131217,#131218,#131219,#131220,#131221,#131222,
#131223,#131224,#131225,#131226,#131227,#131228,#131229,#131230,#131231,
#131232,#131233,#131234,#131235,#131236,#131237,#131238,#131239,#131240,
#131241,#131242,#131243,#131244,#131245,#131246,#131247,#131248,#131249,
#131250,#131251,#131252,#131253,#131254),.UNSPECIFIED.,.F.,.F.,(4,3,3,3,
3,3,3,3,3,3,3,3,3,3,3,3,3,3,3,3,3,3,3,3,4),(32.3317147877909,32.4299572675061,
32.5330903715611,32.631472295279,32.7299238178561,32.8285286698518,32.8424896837258,
32.9410878085162,33.0395455910852,33.1397681589105,33.2380477164451,33.3362942953312,
33.4345373781883,33.5362345670632,33.6346189803181,33.7379725570029,33.8413261336877,
33.9390973941519,34.0367388270572,34.1342810926927,34.2317547370095,34.3292101035806,
34.4266554953363,34.5241539309141,34.5575191894878),.UNSPECIFIED.);
#1275=B_SPLINE_CURVE_WITH_KNOTS('',3,(#131256,#131257,#131258,#131259,#131260,
#131261,#131262,#131263,#131264,#131265,#131266,#131267,#131268,#131269,
#131270,#131271,#131272,#131273,#131274,#131275,#131276,#131277,#131278,
#131279,#131280,#131281,#131282,#131283,#131284,#131285,#131286,#131287,
#131288,#131289,#131290,#131291,#131292,#131293,#131294,#131295,#131296,
#131297,#131298,#131299,#131300,#131301,#131302,#131303,#131304,#131305,
#131306,#131307,#131308,#131309,#131310,#131311,#131312,#131313,#131314,
#131315,#131316,#131317,#131318,#131319,#131320,#131321,#131322,#131323,
#131324,#131325),.UNSPECIFIED.,.F.,.F.,(4,3,3,3,3,3,3,3,3,3,3,3,3,3,3,3,
3,3,3,3,3,3,3,4),(32.3314303398525,32.3776829512062,32.4762810765961,32.5747388598254,
32.6749614274933,32.7732409858351,32.8714875655812,32.9697306493509,33.0714278373052,
33.1698122515945,33.2731658263813,33.3765194011681,33.4751175203003,33.5735752971024,
33.6737978663559,33.7720774178991,33.8703239907224,33.9685670674539,34.0702642633729,
34.1686486704062,34.272002260768,34.3753558511299,34.5238559809544,34.5575191894878),
 .UNSPECIFIED.);
#1276=B_SPLINE_CURVE_WITH_KNOTS('',3,(#131326,#131327,#131328,#131329,#131330,
#131331,#131332,#131333),.UNSPECIFIED.,.F.,.F.,(4,1,1,1,1,4),(34.5575241470784,
35.3741923010918,36.3730287510537,37.3718652010156,38.3707016509774,38.615783154936),
 .UNSPECIFIED.);
#1277=B_SPLINE_CURVE_WITH_KNOTS('',3,(#131339,#131340,#131341,#131342,#131343,
#131344,#131345,#131346,#131347,#131348,#131349,#131350,#131351,#131352,
#131353,#131354,#131355,#131356,#131357,#131358,#131359,#131360,#131361,
#131362,#131363,#131364,#131365,#131366,#131367,#131368,#131369,#131370,
#131371,#131372,#131373,#131374,#131375,#131376,#131377,#131378,#131379,
#131380,#131381,#131382,#131383,#131384,#131385,#131386,#131387,#131388,
#131389,#131390,#131391,#131392,#131393,#131394,#131395,#131396,#131397,
#131398,#131399,#131400,#131401,#131402,#131403,#131404,#131405,#131406,
#131407,#131408,#131409,#131410,#131411,#131412,#131413,#131414,#131415,
#131416,#131417,#131418,#131419,#131420,#131421,#131422,#131423,#131424,
#131425,#131426,#131427,#131428,#131429,#131430,#131431,#131432,#131433,
#131434,#131435,#131436,#131437,#131438,#131439,#131440,#131441,#131442,
#131443,#131444,#131445,#131446,#131447,#131448,#131449,#131450,#131451,
#131452,#131453,#131454,#131455,#131456,#131457,#131458,#131459,#131460,
#131461,#131462),.UNSPECIFIED.,.F.,.F.,(4,3,3,3,3,3,3,3,3,3,3,3,3,3,3,3,
3,3,3,3,3,3,3,3,3,3,3,3,3,3,3,3,3,3,3,3,3,3,3,3,3,4),(40.8407044969197,
40.9391705387198,41.037496428004,41.1368115911763,41.2349607512892,41.3330774110127,
41.4311912274061,41.5313978539002,41.6296531901072,41.7308354617449,41.8320177333826,
41.9306158583836,42.0290736411577,42.129296208931,42.2275757666565,42.3258223457271,
42.424065428763,42.5257626174084,42.6241470308246,42.7275006070845,42.8308541833445,
42.9294523083471,43.0279100911229,43.1281326588958,43.2264122166228,43.3246587956951,
43.4229018787323,43.5245990673758,43.6229834807933,43.7263370570498,43.8296906333064,
43.9282887583114,44.0267465410896,44.1269691088619,44.2252486665915,44.3234952456664,
44.4217383287063,44.5234355173468,44.621819930767,44.7251735070177,44.8285270832683,
44.898397957106),.UNSPECIFIED.);
#1278=B_SPLINE_CURVE_WITH_KNOTS('',3,(#131463,#131464,#131465,#131466,#131467,
#131468,#131469,#131470,#131471,#131472,#131473,#131474,#131475,#131476,
#131477,#131478,#131479,#131480,#131481,#131482,#131483,#131484,#131485,
#131486,#131487,#131488,#131489,#131490,#131491,#131492,#131493,#131494,
#131495,#131496,#131497,#131498,#131499,#131500,#131501,#131502,#131503,
#131504,#131505,#131506,#131507,#131508,#131509,#131510,#131511,#131512,
#131513,#131514,#131515,#131516,#131517,#131518,#131519,#131520,#131521,
#131522,#131523,#131524,#131525,#131526,#131527,#131528,#131529,#131530,
#131531,#131532,#131533,#131534,#131535),.UNSPECIFIED.,.F.,.F.,(4,3,3,3,
3,3,3,3,3,3,3,3,3,3,3,3,3,3,3,3,3,3,3,3,4),(38.6142676516065,38.7127107058196,
38.8113099209326,38.835508383497,38.9341065084865,39.032564291249,39.1327868590252,
39.231066416739,39.3293129957981,39.4275560788223,39.5292532674815,39.6276376808862,
39.7309912571726,39.8343448334589,39.9329429584521,40.0314007412181,40.1316233089935,
40.2299028667105,40.3281494457725,40.4263925287995,40.5280897174548,40.6264741308619,
40.7298277071414,40.8331812834208,40.8407044966674),.UNSPECIFIED.);
#1279=B_SPLINE_CURVE_WITH_KNOTS('',3,(#131537,#131538,#131539,#131540,#131541,
#131542),.UNSPECIFIED.,.F.,.F.,(4,1,1,4),(38.615783154936,39.3695381009393,
40.3683745509012,40.8407024149445),.UNSPECIFIED.);
#1280=B_SPLINE_CURVE_WITH_KNOTS('',3,(#131543,#131544,#131545,#131546,#131547,
#131548,#131549,#131550,#131551,#131552,#131553,#131554,#131555,#131556,
#131557,#131558,#131559,#131560,#131561,#131562,#131563,#131564,#131565,
#131566,#131567,#131568,#131569,#131570,#131571,#131572,#131573,#131574,
#131575,#131576,#131577,#131578,#131579,#131580,#131581,#131582,#131583,
#131584,#131585,#131586,#131587,#131588,#131589,#131590,#131591,#131592,
#131593,#131594,#131595,#131596,#131597,#131598,#131599,#131600,#131601,
#131602,#131603,#131604,#131605,#131606,#131607,#131608,#131609,#131610,
#131611,#131612,#131613,#131614,#131615,#131616,#131617,#131618,#131619,
#131620,#131621,#131622,#131623,#131624,#131625,#131626,#131627,#131628,
#131629,#131630,#131631,#131632,#131633,#131634,#131635,#131636,#131637,
#131638,#131639,#131640,#131641,#131642,#131643,#131644,#131645,#131646,
#131647,#131648,#131649,#131650,#131651,#131652,#131653,#131654,#131655,
#131656,#131657,#131658,#131659,#131660,#131661,#131662,#131663,#131664,
#131665,#131666,#131667,#131668,#131669),.UNSPECIFIED.,.F.,.F.,(4,3,3,3,
3,3,3,3,3,3,3,3,3,3,3,3,3,3,3,3,3,3,3,3,3,3,3,3,3,3,3,3,3,3,3,3,3,3,3,3,
3,3,4),(40.8407044966674,40.9425310419932,41.0487010317106,41.1508691915795,
41.253165848555,41.355678560324,41.3672110008631,41.4658091258526,41.5642669086151,
41.6644894763913,41.7627690341051,41.8610156131641,41.9592586961882,42.0609558848474,
42.1593402982522,42.2626938745385,42.3660474508249,42.4646455758181,42.5631033585841,
42.6633259263595,42.7616054840764,42.8598520631385,42.9580951461656,43.0597923348209,
43.1581767482281,43.2615303245075,43.3648839007868,43.4634820258002,43.561939808587,
43.6621623763572,43.7604419340954,43.858688513179,43.9569315962279,44.0586287848581,
44.1570131982872,44.260366774518,44.3637203507487,44.462314022054,44.5607732131585,
44.6591152246784,44.7573894748803,44.8556332863466,44.8979422931065),
 .UNSPECIFIED.);
#1281=B_SPLINE_CURVE_WITH_KNOTS('',3,(#131675,#131676,#131677,#131678,#131679,
#131680,#131681,#131682),.UNSPECIFIED.,.F.,.F.,(4,1,1,1,1,4),(47.123889803847,
47.8250364331539,48.8238728831158,49.8227093330776,50.8215457830395,51.1819113926155),
 .UNSPECIFIED.);
#1282=B_SPLINE_CURVE_WITH_KNOTS('',3,(#131683,#131684,#131685,#131686,#131687,
#131688,#131689,#131690,#131691,#131692,#131693,#131694,#131695,#131696,
#131697,#131698,#131699,#131700,#131701,#131702,#131703,#131704,#131705,
#131706,#131707,#131708,#131709,#131710,#131711,#131712,#131713,#131714,
#131715,#131716,#131717,#131718,#131719,#131720,#131721,#131722,#131723,
#131724,#131725,#131726,#131727,#131728,#131729,#131730,#131731,#131732,
#131733,#131734,#131735,#131736,#131737,#131738,#131739,#131740,#131741,
#131742,#131743,#131744,#131745,#131746,#131747,#131748,#131749,#131750,
#131751,#131752),.UNSPECIFIED.,.F.,.F.,(4,3,3,3,3,3,3,3,3,3,3,3,3,3,3,3,
3,3,3,3,3,3,3,4),(44.898397957106,44.9968932559775,45.0952714816404,45.1935672870477,
45.2918209506617,45.3900619643857,45.4883197993756,45.5866859408243,45.6851136892991,
45.7837031645335,45.8273635332301,45.9259616582337,46.0244194410106,46.1246420087832,
46.2229215665112,46.3211681455843,46.4194112286229,46.5211084172651,46.619492830684,
46.722846406938,46.826199983192,46.9466622822371,47.0654828012668,47.1238896269795),
 .UNSPECIFIED.);
#1283=B_SPLINE_CURVE_WITH_KNOTS('',3,(#131754,#131755,#131756,#131757,#131758,
#131759,#131760,#131761,#131762,#131763,#131764,#131765,#131766,#131767,
#131768,#131769,#131770,#131771,#131772,#131773,#131774,#131775,#131776,
#131777,#131778,#131779,#131780,#131781,#131782,#131783,#131784,#131785,
#131786,#131787,#131788,#131789,#131790,#131791,#131792,#131793,#131794,
#131795,#131796,#131797,#131798,#131799,#131800,#131801,#131802,#131803,
#131804,#131805,#131806,#131807,#131808,#131809,#131810,#131811,#131812,
#131813,#131814,#131815,#131816,#131817,#131818,#131819,#131820,#131821,
#131822,#131823),.UNSPECIFIED.,.F.,.F.,(4,3,3,3,3,3,3,3,3,3,3,3,3,3,3,3,
3,3,3,3,3,3,3,4),(44.8979422931065,44.996192493912,45.0945462233762,45.1929541967959,
45.2915321292331,45.3625568007106,45.4611549257132,45.5596127084888,45.6598352762618,
45.7581148339886,45.8563614130606,45.9546044960977,46.0563016847413,46.1546860981588,
46.2580396744156,46.3613932506724,46.4587199838046,46.5559210250952,46.6530274701205,
46.750070296518,46.8471124553622,46.9441490048065,47.0412721236584,47.123889803847),
 .UNSPECIFIED.);
#1284=B_SPLINE_CURVE_WITH_KNOTS('',3,(#131824,#131825,#131826,#131827,#131828,
#131829,#131830,#131831),.UNSPECIFIED.,.F.,.F.,(4,1,1,1,1,4),(47.1238901029355,
47.3602297006343,48.3590661505962,49.3579026005581,50.3567390505199,51.1803881837399),
 .UNSPECIFIED.);
#1285=B_SPLINE_CURVE_WITH_KNOTS('',3,(#131837,#131838,#131839,#131840,#131841,
#131842,#131843,#131844,#131845,#131846,#131847,#131848,#131849,#131850,
#131851,#131852,#131853,#131854,#131855,#131856,#131857,#131858,#131859,
#131860,#131861,#131862,#131863,#131864,#131865,#131866,#131867,#131868,
#131869,#131870,#131871,#131872,#131873,#131874,#131875,#131876,#131877,
#131878,#131879,#131880,#131881,#131882,#131883,#131884,#131885,#131886,
#131887,#131888,#131889,#131890,#131891,#131892,#131893,#131894,#131895,
#131896,#131897,#131898,#131899,#131900,#131901,#131902,#131903,#131904,
#131905,#131906,#131907,#131908,#131909,#131910,#131911,#131912,#131913,
#131914,#131915,#131916,#131917,#131918,#131919,#131920,#131921,#131922,
#131923,#131924,#131925,#131926,#131927,#131928,#131929,#131930,#131931,
#131932,#131933,#131934,#131935,#131936,#131937,#131938,#131939,#131940,
#131941,#131942,#131943,#131944,#131945,#131946,#131947,#131948,#131949,
#131950,#131951,#131952,#131953,#131954,#131955,#131956,#131957,#131958,
#131959,#131960),.UNSPECIFIED.,.F.,.F.,(4,3,3,3,3,3,3,3,3,3,3,3,3,3,3,3,
3,3,3,3,3,3,3,3,3,3,3,3,3,3,3,3,3,3,3,3,3,3,3,3,3,4),(53.4070755243489,
53.5149520672591,53.6231638610545,53.7318758460054,53.8180551329251,53.9166532579288,
54.0151110407055,54.1153336084782,54.2136131662063,54.3118597452796,54.4101028283181,
54.5118000169604,54.6101844303791,54.7135380066331,54.816891582887,54.9154897078907,
55.0139474906675,55.1141700584402,55.2124496161683,55.3106961952417,55.4089392782802,
55.5106364669224,55.6090208803412,55.7123744565951,55.8157280328489,55.9143261578526,
56.0127839406294,56.1130065084021,56.2112860661302,56.3095326452036,56.4077757282421,
56.5094729168843,56.6078573303031,56.7112109065569,56.8145644828108,56.913145227458,
57.0115945031628,57.1099420320524,57.2082227592543,57.3064633876106,57.404720555686,
57.463995963324),.UNSPECIFIED.);
#1286=B_SPLINE_CURVE_WITH_KNOTS('',3,(#131961,#131962,#131963,#131964,#131965,
#131966),.UNSPECIFIED.,.F.,.F.,(4,1,1,4),(51.1819113926155,51.8203822330014,
52.8192186829633,53.4070751110266),.UNSPECIFIED.);
#1287=B_SPLINE_CURVE_WITH_KNOTS('',3,(#131968,#131969,#131970,#131971,#131972,
#131973,#131974),.UNSPECIFIED.,.F.,.F.,(4,1,1,1,4),(51.1803881837399,51.3555755004818,
52.3544119504437,53.3532484004055,53.4070751110266),.UNSPECIFIED.);
#1288=B_SPLINE_CURVE_WITH_KNOTS('',3,(#131975,#131976,#131977,#131978,#131979,
#131980,#131981,#131982,#131983,#131984,#131985,#131986,#131987,#131988,
#131989,#131990,#131991,#131992,#131993,#131994,#131995,#131996,#131997,
#131998,#131999,#132000,#132001,#132002,#132003,#132004,#132005,#132006,
#132007,#132008,#132009,#132010,#132011,#132012,#132013,#132014,#132015,
#132016,#132017,#132018,#132019,#132020,#132021,#132022,#132023,#132024,
#132025,#132026,#132027,#132028,#132029,#132030,#132031,#132032,#132033,
#132034,#132035,#132036,#132037,#132038,#132039,#132040,#132041,#132042,
#132043,#132044,#132045,#132046,#132047,#132048,#132049,#132050,#132051,
#132052,#132053,#132054,#132055,#132056,#132057,#132058,#132059,#132060,
#132061,#132062,#132063,#132064,#132065,#132066,#132067,#132068,#132069,
#132070,#132071,#132072,#132073,#132074,#132075,#132076,#132077,#132078,
#132079,#132080,#132081,#132082,#132083,#132084,#132085,#132086,#132087,
#132088,#132089,#132090,#132091,#132092,#132093,#132094,#132095,#132096,
#132097,#132098,#132099,#132100,#132101),.UNSPECIFIED.,.F.,.F.,(4,3,3,3,
3,3,3,3,3,3,3,3,3,3,3,3,3,3,3,3,3,3,3,3,3,3,3,3,3,3,3,3,3,3,3,3,3,3,3,3,
3,3,4),(53.4070751110266,53.5048543854907,53.6024983707771,53.7000367768844,
53.7975186210124,53.8949743677961,53.9924344477706,54.0899931990357,54.1876041339867,
54.2853815723762,54.3520848503674,54.4506829753711,54.549140758148,54.6493633259206,
54.7476428836488,54.8458894627222,54.9441325457611,55.0458297344031,55.1442141478219,
55.2475677240756,55.3509213003293,55.4495194253329,55.5479772081095,55.6481997758822,
55.7464793336103,55.8447259126838,55.9429689957221,56.0446661843644,56.1430505977832,
56.2464041740372,56.3497577502912,56.4483558752949,56.5468136580716,56.6470362258442,
56.7453157835724,56.8435623626457,56.9418054456843,57.0435026343265,57.1418870477453,
57.2452406239991,57.348594200253,57.4471969426027,57.464911377198),
 .UNSPECIFIED.);
#1289=B_SPLINE_CURVE_WITH_KNOTS('',3,(#132107,#132108,#132109,#132110,#132111,
#132112,#132113,#132114),.UNSPECIFIED.,.F.,.F.,(4,1,1,1,1,4),(59.6902604182062,
59.8110738326964,60.8099102826583,61.8087467326201,62.807583182582,63.7472418106748),
 .UNSPECIFIED.);
#1290=B_SPLINE_CURVE_WITH_KNOTS('',3,(#132115,#132116,#132117,#132118,#132119,
#132120,#132121,#132122,#132123,#132124,#132125,#132126,#132127,#132128,
#132129,#132130,#132131,#132132,#132133,#132134,#132135,#132136,#132137,
#132138,#132139,#132140,#132141,#132142,#132143,#132144,#132145,#132146,
#132147,#132148,#132149,#132150,#132151,#132152,#132153,#132154,#132155,
#132156,#132157,#132158,#132159,#132160,#132161,#132162,#132163,#132164,
#132165,#132166,#132167,#132168,#132169,#132170,#132171,#132172,#132173,
#132174,#132175,#132176,#132177,#132178,#132179,#132180,#132181,#132182,
#132183,#132184),.UNSPECIFIED.,.F.,.F.,(4,3,3,3,3,3,3,3,3,3,3,3,3,3,3,3,
3,3,3,3,3,3,3,4),(57.463995963324,57.5623571570582,57.6607771651584,57.7593619663573,
57.8134009327726,57.9119990577763,58.010456840553,58.1106794083257,58.2089589660538,
58.3072055451272,58.4054486281658,58.507145816808,58.6055302302267,58.7088838064806,
58.8122373827345,58.9094791608007,59.0070768179764,59.1040671063403,59.2009981633324,
59.2979009849175,59.3959908432397,59.4929780422904,59.5916192302483,59.6902604182062),
 .UNSPECIFIED.);
#1291=B_SPLINE_CURVE_WITH_KNOTS('',3,(#132186,#132187,#132188,#132189,#132190,
#132191,#132192,#132193,#132194,#132195,#132196,#132197,#132198,#132199,
#132200,#132201,#132202,#132203,#132204,#132205,#132206,#132207,#132208,
#132209,#132210,#132211,#132212,#132213,#132214,#132215,#132216,#132217,
#132218,#132219,#132220,#132221,#132222,#132223,#132224,#132225,#132226,
#132227,#132228,#132229,#132230,#132231,#132232,#132233,#132234,#132235,
#132236,#132237,#132238,#132239,#132240,#132241,#132242,#132243,#132244,
#132245,#132246,#132247,#132248,#132249,#132250,#132251,#132252),
 .UNSPECIFIED.,.F.,.F.,(4,3,3,3,3,3,3,3,3,3,3,3,3,3,3,3,3,3,3,3,3,3,4),
(57.464911377198,57.5633474036735,57.6616774189312,57.7599496840526,57.8581937126486,
57.956438983539,58.0547832757564,58.1531751763202,58.2517448625486,58.3474306502149,
58.4460287752185,58.5444865579953,58.644709125768,58.7429886834961,58.8412352625696,
58.9394783456082,59.0411755342503,59.1395599476692,59.242913523923,59.3462671001768,
59.460882914029,59.5755716660042,59.6902604179793),.UNSPECIFIED.);
#1292=B_SPLINE_CURVE_WITH_KNOTS('',3,(#132253,#132254,#132255,#132256,#132257,
#132258,#132259,#132260,#132261,#132262,#132263,#132264,#132265,#132266,
#132267,#132268,#132269,#132270,#132271,#132272,#132273,#132274,#132275,
#132276,#132277,#132278,#132279,#132280,#132281,#132282,#132283,#132284,
#132285,#132286,#132287,#132288,#132289,#132290,#132291,#132292,#132293,
#132294,#132295,#132296,#132297,#132298,#132299,#132300,#132301,#132302,
#132303,#132304,#132305,#132306,#132307,#132308,#132309,#132310,#132311,
#132312,#132313,#132314,#132315,#132316,#132317,#132318,#132319,#132320,
#132321,#132322,#132323,#132324,#132325,#132326,#132327,#132328,#132329,
#132330,#132331,#132332,#132333,#132334,#132335,#132336,#132337,#132338,
#132339,#132340,#132341,#132342,#132343,#132344,#132345,#132346,#132347,
#132348,#132349,#132350,#132351,#132352,#132353,#132354,#132355,#132356,
#132357,#132358,#132359,#132360,#132361,#132362,#132363,#132364,#132365,
#132366,#132367,#132368,#132369,#132370,#132371,#132372,#132373,#132374,
#132375,#132376),.UNSPECIFIED.,.F.,.F.,(4,3,3,3,3,3,3,3,3,3,3,3,3,3,3,3,
3,3,3,3,3,3,3,3,3,3,3,3,3,3,3,3,3,3,3,3,3,3,3,3,3,4),(59.6902604182062,
59.788634173056,59.8869985815969,59.985382791999,60.0838846667639,60.1824499292132,
60.2811933482969,60.3451035501387,60.4437016751424,60.542159457919,60.6423820256917,
60.7406615834199,60.8389081624933,60.9371512455318,61.0388484341739,61.1372328475928,
61.2405864238466,61.3439400001005,61.4425381251042,61.5409959078811,61.6412184756537,
61.7394980333819,61.8377446124552,61.9359876954937,62.0376848841359,62.1360692975546,
62.2394228738085,62.3427764500624,62.4413745750661,62.5398323578432,62.6400549256158,
62.738334483344,62.8365810624174,62.9348241454559,63.036521334098,63.1349057475167,
63.2382593237705,63.3416129000243,63.4431811229531,63.5416227638002,63.6447542777698,
63.7478857917395),.UNSPECIFIED.);
#1293=B_SPLINE_CURVE_WITH_KNOTS('',3,(#132382,#132383,#132384,#132385,#132386,
#132387,#132388,#132389,#132390,#132391,#132392,#132393,#132394,#132395,
#132396,#132397,#132398,#132399,#132400,#132401,#132402,#132403,#132404,
#132405,#132406,#132407,#132408,#132409,#132410,#132411,#132412,#132413,
#132414,#132415,#132416,#132417,#132418,#132419,#132420,#132421,#132422,
#132423,#132424,#132425,#132426,#132427,#132428,#132429,#132430,#132431,
#132432,#132433,#132434,#132435,#132436,#132437,#132438,#132439,#132440,
#132441,#132442,#132443,#132444,#132445,#132446,#132447,#132448,#132449,
#132450,#132451,#132452,#132453,#132454,#132455,#132456,#132457,#132458,
#132459,#132460,#132461,#132462,#132463,#132464,#132465,#132466,#132467,
#132468,#132469,#132470,#132471,#132472,#132473,#132474,#132475,#132476,
#132477,#132478,#132479,#132480,#132481,#132482,#132483,#132484,#132485,
#132486,#132487,#132488,#132489,#132490,#132491,#132492,#132493,#132494,
#132495,#132496,#132497,#132498,#132499,#132500,#132501,#132502,#132503,
#132504,#132505,#132506,#132507,#132508),.UNSPECIFIED.,.F.,.F.,(4,3,3,3,
3,3,3,3,3,3,3,3,3,3,3,3,3,3,3,3,3,3,3,3,3,3,3,3,3,3,3,3,3,3,3,3,3,3,3,3,
3,3,4),(65.9734457253857,66.0704340596178,66.1673127975359,66.2641328887561,
66.3609254267911,66.4577214670339,66.5546134226803,66.6515579893417,66.7486626585401,
66.8029289824295,66.9015271074332,66.99998489021,67.1002074579826,67.1984870157107,
67.2967335947841,67.3949766778227,67.4966738664648,67.5950582798837,67.6984118561375,
67.8017654323914,67.9003635573952,67.9988213401717,68.0990439079444,68.1973234656725,
68.2955700447459,68.3938131277845,68.4955103164266,68.5938947298455,68.6972483060993,
68.8006018823532,68.8992000073569,68.9976577901335,69.0978803579062,69.1961599156345,
69.2944064947079,69.3926495777463,69.4943467663885,69.5927311798073,69.6960847560612,
69.7994383323151,69.8980412657762,69.996491840234,70.0313849422026),
 .UNSPECIFIED.);
#1294=B_SPLINE_CURVE_WITH_KNOTS('',3,(#132509,#132510,#132511,#132512,#132513,
#132514,#132515),.UNSPECIFIED.,.F.,.F.,(4,1,1,1,4),(63.7472418106748,63.8064196325439,
64.8052560825058,65.8040925324676,65.9734457253857),.UNSPECIFIED.);
#1295=B_SPLINE_CURVE_WITH_KNOTS('',3,(#132517,#132518,#132519,#132520,#132521,
#132522,#132523,#132524,#132525,#132526,#132527,#132528,#132529,#132530,
#132531,#132532,#132533,#132534,#132535,#132536,#132537,#132538,#132539,
#132540,#132541,#132542,#132543,#132544,#132545,#132546,#132547,#132548,
#132549,#132550,#132551,#132552,#132553,#132554,#132555,#132556,#132557,
#132558,#132559,#132560,#132561,#132562,#132563,#132564,#132565,#132566,
#132567,#132568,#132569,#132570,#132571,#132572,#132573,#132574,#132575,
#132576,#132577,#132578,#132579,#132580,#132581,#132582,#132583,#132584,
#132585,#132586),.UNSPECIFIED.,.F.,.F.,(4,3,3,3,3,3,3,3,3,3,3,3,3,3,3,3,
3,3,3,3,3,3,3,4),(63.7478857917395,63.8461305577829,63.9443750416371,64.0433936187244,
64.1417828184941,64.2411160842401,64.3404493499862,64.43904747499,64.5375052577667,
64.6377278255393,64.7360073832675,64.8342539623408,64.9324970453792,65.0341942340214,
65.1325786474403,65.2359322236941,65.339285799948,65.4384637976082,65.5374980774499,
65.6364173808601,65.7352455972602,65.8340208922134,65.9327849002204,65.9734457253857),
 .UNSPECIFIED.);
#1296=B_SPLINE_CURVE_WITH_KNOTS('',3,(#132587,#132588,#132589,#132590,#132591,
#132592,#132593,#132594,#132595,#132596,#132597,#132598,#132599,#132600,
#132601,#132602,#132603,#132604,#132605,#132606,#132607,#132608,#132609,
#132610,#132611,#132612,#132613,#132614,#132615,#132616,#132617,#132618,
#132619,#132620,#132621,#132622,#132623,#132624,#132625,#132626,#132627,
#132628,#132629,#132630,#132631,#132632,#132633,#132634,#132635,#132636,
#132637,#132638,#132639,#132640,#132641,#132642,#132643,#132644,#132645,
#132646,#132647,#132648,#132649,#132650,#132651,#132652,#132653,#132654,
#132655,#132656,#132657,#132658,#132659,#132660,#132661,#132662,#132663,
#132664,#132665,#132666,#132667,#132668,#132669,#132670,#132671,#132672,
#132673,#132674,#132675,#132676,#132677,#132678,#132679,#132680,#132681,
#132682,#132683,#132684,#132685,#132686,#132687,#132688,#132689,#132690,
#132691,#132692,#132693,#132694,#132695,#132696,#132697,#132698,#132699,
#132700,#132701,#132702,#132703,#132704,#132705,#132706,#132707,#132708,
#132709,#132710),.UNSPECIFIED.,.F.,.F.,(4,3,3,3,3,3,3,3,3,3,3,3,3,3,3,3,
3,3,3,3,3,3,3,3,3,3,3,3,3,3,3,3,3,3,3,3,3,3,3,3,3,4),(65.9734457256204,
66.0848798050745,66.1968635637055,66.3094957826849,66.3381222499099,66.4367203749136,
66.5351781576904,66.635400725463,66.7336802831912,66.8319268622646,66.9301699453032,
67.0318671339454,67.1302515473642,67.233605123618,67.3369586998718,67.4355568248755,
67.5340146076523,67.634237175425,67.7325167331531,67.8307633122265,67.929006395265,
68.0307035839072,68.129087997326,68.2324415735798,68.3357951498337,68.4343932748374,
68.5328510576141,68.6330736253868,68.7313531831149,68.8295997621883,68.9278428452268,
69.029540033869,69.1279244472878,69.2312780235416,69.3346315997955,69.4332079436479,
69.5316540255028,69.6299995615628,69.7300683995431,69.8283147700062,69.929294841745,
70.0302749134839),.UNSPECIFIED.);
#1297=B_SPLINE_CURVE_WITH_KNOTS('',3,(#132716,#132717,#132718,#132719,#132720,
#132721,#132722,#132723),.UNSPECIFIED.,.F.,.F.,(4,1,1,1,1,4),(72.2566310325654,
72.7959476822007,73.7947841321626,74.7936205821245,75.7924570320864,76.3138574458811),
 .UNSPECIFIED.);
#1298=B_SPLINE_CURVE_WITH_KNOTS('',3,(#132724,#132725,#132726,#132727,#132728,
#132729,#132730,#132731,#132732,#132733,#132734,#132735,#132736,#132737,
#132738,#132739,#132740,#132741,#132742,#132743,#132744,#132745,#132746,
#132747,#132748,#132749,#132750,#132751,#132752,#132753,#132754,#132755,
#132756,#132757,#132758,#132759,#132760,#132761,#132762,#132763,#132764,
#132765,#132766,#132767,#132768,#132769,#132770,#132771,#132772,#132773,
#132774,#132775,#132776,#132777,#132778,#132779,#132780,#132781,#132782,
#132783,#132784,#132785,#132786,#132787,#132788,#132789,#132790,#132791,
#132792,#132793),.UNSPECIFIED.,.F.,.F.,(4,3,3,3,3,3,3,3,3,3,3,3,3,3,3,3,
3,3,3,3,3,3,3,4),(70.0313849422026,70.1297027318843,70.2279679340465,70.3262100542967,
70.4244585681002,70.5228092667787,70.6212122014149,70.7197874226758,70.798274782277,
70.8968729072807,70.9953306900576,71.0955532578302,71.1938328155585,71.2920793946319,
71.3903224776702,71.4920196663123,71.5904040797312,71.693757655985,71.7971112322389,
71.9028340905518,72.0081993817381,72.1133399321502,72.2181701837247,72.2566308185864),
 .UNSPECIFIED.);
#1299=B_SPLINE_CURVE_WITH_KNOTS('',3,(#132795,#132796,#132797,#132798,#132799,
#132800,#132801,#132802,#132803,#132804,#132805,#132806,#132807,#132808,
#132809,#132810,#132811,#132812,#132813,#132814,#132815,#132816,#132817,
#132818,#132819,#132820,#132821,#132822,#132823,#132824,#132825,#132826,
#132827,#132828,#132829,#132830,#132831,#132832,#132833,#132834,#132835,
#132836,#132837,#132838,#132839,#132840,#132841,#132842,#132843,#132844,
#132845,#132846,#132847,#132848,#132849,#132850,#132851,#132852,#132853,
#132854,#132855,#132856,#132857,#132858,#132859,#132860,#132861,#132862,
#132863,#132864),.UNSPECIFIED.,.F.,.F.,(4,3,3,3,3,3,3,3,3,3,3,3,3,3,3,3,
3,3,3,3,3,3,3,4),(70.0302749134839,70.1286604417134,70.2310642457354,70.3334680497574,
70.4320661747611,70.5305239575379,70.6307465253105,70.7290260830387,70.8272726621121,
70.9255157451505,71.0272129337927,71.1255973472116,71.2289509234654,71.3323044997193,
71.4298807240689,71.5273176349422,71.6246428433671,71.7219081150621,71.8191441424517,
71.9163815796696,72.0137087835221,72.1110862397607,72.2086145464313,72.2566310325654),
 .UNSPECIFIED.);
#1300=B_SPLINE_CURVE_WITH_KNOTS('',3,(#132865,#132866,#132867,#132868,#132869,
#132870,#132871,#132872),.UNSPECIFIED.,.F.,.F.,(4,1,1,1,1,4),(72.2566310325654,
72.3311409496812,73.329977399643,74.3288138496049,75.3276502995668,76.3138964032405),
 .UNSPECIFIED.);
#1301=B_SPLINE_CURVE_WITH_KNOTS('',3,(#132878,#132879,#132880,#132881,#132882,
#132883,#132884,#132885,#132886,#132887,#132888,#132889,#132890,#132891,
#132892,#132893,#132894,#132895,#132896,#132897,#132898,#132899,#132900,
#132901,#132902,#132903,#132904,#132905,#132906,#132907,#132908,#132909,
#132910,#132911,#132912,#132913,#132914,#132915,#132916,#132917,#132918,
#132919,#132920,#132921,#132922,#132923,#132924,#132925,#132926,#132927,
#132928,#132929,#132930,#132931,#132932,#132933,#132934,#132935,#132936,
#132937,#132938,#132939,#132940,#132941,#132942,#132943,#132944,#132945,
#132946,#132947,#132948,#132949,#132950,#132951,#132952,#132953,#132954,
#132955,#132956,#132957,#132958,#132959,#132960,#132961,#132962,#132963,
#132964,#132965,#132966,#132967,#132968,#132969,#132970,#132971,#132972,
#132973,#132974,#132975,#132976,#132977,#132978,#132979,#132980,#132981,
#132982,#132983,#132984,#132985,#132986,#132987,#132988,#132989,#132990,
#132991,#132992,#132993,#132994,#132995,#132996,#132997,#132998,#132999,
#133000,#133001),.UNSPECIFIED.,.F.,.F.,(4,3,3,3,3,3,3,3,3,3,3,3,3,3,3,3,
3,3,3,3,3,3,3,3,3,3,3,3,3,3,3,3,3,3,3,3,3,3,3,3,3,4),(78.5398164397795,
78.6677108218205,78.788966381972,78.8875645069757,78.9860222897525,79.0862448575251,
79.1845244152533,79.2827709943266,79.381014077365,79.4827112660072,79.581095679426,
79.68444925568,79.7878028319339,79.8864009569376,79.9848587397144,80.0850813074871,
80.1833608652152,80.2816074442886,80.379850527327,80.4815477159692,80.579932129388,
80.6832857056419,80.7866392818957,80.8852374068994,80.9836951896762,81.0839177574489,
81.182197315177,81.2804438942504,81.3786869772889,81.480384165931,81.5787685793498,
81.6821221556037,81.7854757318576,81.8868624824842,81.9852993415052,82.0836395026602,
82.1819125647065,82.2801480543488,82.3784063402449,82.4766798066968,82.5750348018018,
82.5965697368708),.UNSPECIFIED.);
#1302=B_SPLINE_CURVE_WITH_KNOTS('',3,(#133002,#133003,#133004,#133005,#133006,
#133007),.UNSPECIFIED.,.F.,.F.,(4,1,1,4),(76.3138574458811,76.7912934820482,
77.7901299320101,78.539816339745),.UNSPECIFIED.);
#1303=B_SPLINE_CURVE_WITH_KNOTS('',3,(#133009,#133010,#133011,#133012,#133013,
#133014,#133015),.UNSPECIFIED.,.F.,.F.,(4,1,1,1,4),(76.3138964032405,76.3264867495287,
77.3253231994905,78.3241596494524,78.539816339745),.UNSPECIFIED.);
#1304=B_SPLINE_CURVE_WITH_KNOTS('',3,(#133016,#133017,#133018,#133019,#133020,
#133021,#133022,#133023,#133024,#133025,#133026,#133027,#133028,#133029,
#133030,#133031,#133032,#133033,#133034,#133035,#133036,#133037,#133038,
#133039,#133040,#133041,#133042,#133043,#133044,#133045,#133046,#133047,
#133048,#133049,#133050,#133051,#133052,#133053,#133054,#133055,#133056,
#133057,#133058,#133059,#133060,#133061,#133062,#133063,#133064,#133065,
#133066,#133067,#133068,#133069,#133070,#133071,#133072,#133073,#133074,
#133075,#133076,#133077,#133078,#133079,#133080,#133081,#133082,#133083,
#133084,#133085,#133086,#133087,#133088,#133089,#133090,#133091,#133092,
#133093,#133094,#133095,#133096,#133097,#133098,#133099,#133100,#133101,
#133102,#133103,#133104,#133105,#133106,#133107,#133108,#133109,#133110,
#133111,#133112,#133113,#133114,#133115,#133116,#133117,#133118,#133119,
#133120,#133121,#133122,#133123,#133124,#133125,#133126,#133127,#133128,
#133129,#133130,#133131,#133132,#133133,#133134,#133135,#133136,#133137,
#133138,#133139),.UNSPECIFIED.,.F.,.F.,(4,3,3,3,3,3,3,3,3,3,3,3,3,3,3,3,
3,3,3,3,3,3,3,3,3,3,3,3,3,3,3,3,3,3,3,3,3,3,3,3,3,4),(78.539816339745,78.6377138097037,
78.7346673304385,78.8315786913981,78.9284788661295,79.0271081744507,79.124135318513,
79.2235657089636,79.3229960994143,79.421594224418,79.5200520071948,79.6202745749675,
79.7185541326956,79.816800711769,79.9150437948074,80.0167409834496,80.1151253968684,
80.2184789731223,80.3218325493762,80.4204306743799,80.5188884571566,80.6191110249293,
80.7173905826575,80.8156371617309,80.9138802447692,81.0155774334114,81.1139618468302,
81.2173154230841,81.320668999338,81.4192671243417,81.5177249071183,81.617947474891,
81.7162270326191,81.8144736116923,81.9127166947308,82.0144138833731,82.1127982967919,
82.2161518730459,82.3195054492999,82.4180964129972,82.5165362141383,82.5977152782637),
 .UNSPECIFIED.);
#1305=B_SPLINE_CURVE_WITH_KNOTS('',3,(#133145,#133146,#133147,#133148,#133149,
#133150,#133151,#133152),.UNSPECIFIED.,.F.,.F.,(4,1,1,1,1,4),(84.8230070322059,
85.7808215317051,86.779657981667,87.7784944316288,88.7773308815907,88.8809435586522),
 .UNSPECIFIED.);
#1306=B_SPLINE_CURVE_WITH_KNOTS('',3,(#133153,#133154,#133155,#133156,#133157,
#133158,#133159,#133160,#133161,#133162,#133163,#133164,#133165,#133166,
#133167,#133168,#133169,#133170,#133171,#133172,#133173,#133174,#133175,
#133176,#133177,#133178,#133179,#133180,#133181,#133182,#133183,#133184,
#133185,#133186,#133187,#133188,#133189,#133190,#133191,#133192,#133193,
#133194,#133195,#133196,#133197,#133198,#133199,#133200,#133201,#133202,
#133203,#133204,#133205,#133206,#133207,#133208,#133209,#133210,#133211,
#133212,#133213,#133214,#133215,#133216,#133217,#133218,#133219,#133220,
#133221,#133222),.UNSPECIFIED.,.F.,.F.,(4,3,3,3,3,3,3,3,3,3,3,3,3,3,3,3,
3,3,3,3,3,3,3,4),(82.5965697368708,82.6951414027961,82.7843121818195,82.8829103068232,
82.9813680896,83.0815906573726,83.1798702151008,83.2781167941742,83.3763598772127,
83.4780570658548,83.5764414792737,83.6797950555275,83.7831486317814,83.8817467567851,
83.9802045395619,84.0804271073345,84.1787066650626,84.276953244136,84.3751963271744,
84.4768935158166,84.5752779292354,84.6786315054893,84.7819850817432,84.8230016469246),
 .UNSPECIFIED.);
#1307=B_SPLINE_CURVE_WITH_KNOTS('',3,(#133224,#133225,#133226,#133227,#133228,
#133229,#133230,#133231,#133232,#133233,#133234,#133235,#133236,#133237,
#133238,#133239,#133240,#133241,#133242,#133243,#133244,#133245,#133246,
#133247,#133248,#133249,#133250,#133251,#133252,#133253,#133254,#133255,
#133256,#133257,#133258,#133259,#133260,#133261,#133262,#133263,#133264,
#133265,#133266,#133267,#133268,#133269,#133270,#133271,#133272,#133273,
#133274,#133275,#133276,#133277,#133278,#133279,#133280,#133281,#133282,
#133283,#133284,#133285,#133286,#133287,#133288,#133289,#133290,#133291,
#133292,#133293),.UNSPECIFIED.,.F.,.F.,(4,3,3,3,3,3,3,3,3,3,3,3,3,3,3,3,
3,3,3,3,3,3,3,4),(82.5977152782637,82.6960046491985,82.7942553193272,82.8924967767674,
82.9907584919828,83.0891304482576,83.1875671008218,83.2861621677909,83.3183418992618,
83.4169400242655,83.5153978070424,83.6156203748151,83.7138999325432,83.8121465116165,
83.9103895946546,84.0120867832969,84.1104711967158,84.2138247729697,84.3171783492237,
84.4205578302507,84.5236543867489,84.6265834813182,84.7292989065995,84.8230016469246),
 .UNSPECIFIED.);
#1308=B_SPLINE_CURVE_WITH_KNOTS('',3,(#133294,#133295,#133296,#133297,#133298,
#133299,#133300,#133301,#133302,#133303,#133304,#133305,#133306,#133307,
#133308,#133309,#133310,#133311,#133312,#133313,#133314,#133315,#133316,
#133317,#133318,#133319,#133320,#133321,#133322,#133323,#133324,#133325,
#133326,#133327,#133328,#133329,#133330,#133331,#133332,#133333,#133334,
#133335,#133336,#133337,#133338,#133339,#133340,#133341,#133342,#133343,
#133344,#133345,#133346,#133347,#133348,#133349,#133350,#133351,#133352,
#133353,#133354,#133355,#133356,#133357,#133358,#133359,#133360,#133361,
#133362,#133363,#133364,#133365,#133366,#133367,#133368,#133369,#133370,
#133371,#133372,#133373,#133374,#133375,#133376,#133377,#133378,#133379,
#133380,#133381,#133382,#133383,#133384,#133385,#133386,#133387,#133388,
#133389,#133390,#133391,#133392,#133393,#133394,#133395,#133396,#133397,
#133398,#133399,#133400,#133401,#133402,#133403,#133404,#133405,#133406,
#133407,#133408,#133409,#133410,#133411,#133412,#133413,#133414,#133415,
#133416,#133417),.UNSPECIFIED.,.F.,.F.,(4,3,3,3,3,3,3,3,3,3,3,3,3,3,3,3,
3,3,3,3,3,3,3,3,3,3,3,3,3,3,3,3,3,3,3,3,3,3,3,3,3,4),(84.8230016472006,
84.9261861619504,85.0296647966981,85.1332945907093,85.2372126194225,85.3160147991855,
85.4146129241892,85.513070706966,85.6132932747387,85.7115728324668,85.8098194115402,
85.9080624945788,86.009759683221,86.1081440966398,86.2114976728936,86.3148512491474,
86.4134493741511,86.5119071569279,86.6121297247005,86.7104092824287,86.8086558615021,
86.9068989445406,87.0085961331828,87.1069805466016,87.2103341228555,87.3136876991093,
87.412285824113,87.5107436068897,87.6109661746624,87.7092457323906,87.8074923114639,
87.9057353945024,88.0074325831446,88.1058169965634,88.2091705728173,88.3125241490712,
88.411113786503,88.5095698168581,88.6079122101868,88.7061871882877,88.8044419893942,
88.8801389537999),.UNSPECIFIED.);
#1309=B_SPLINE_CURVE_WITH_KNOTS('',3,(#133423,#133424,#133425,#133426,#133427,
#133428,#133429,#133430,#133431,#133432,#133433,#133434,#133435,#133436,
#133437,#133438,#133439,#133440,#133441,#133442,#133443,#133444,#133445,
#133446,#133447,#133448,#133449,#133450,#133451,#133452,#133453,#133454,
#133455,#133456,#133457,#133458,#133459,#133460,#133461,#133462,#133463,
#133464,#133465,#133466,#133467,#133468,#133469,#133470,#133471,#133472,
#133473,#133474,#133475,#133476,#133477,#133478,#133479,#133480,#133481,
#133482,#133483,#133484,#133485,#133486,#133487,#133488,#133489,#133490,
#133491,#133492,#133493,#133494,#133495,#133496,#133497,#133498,#133499,
#133500,#133501,#133502,#133503,#133504,#133505,#133506,#133507,#133508,
#133509,#133510,#133511,#133512,#133513,#133514,#133515,#133516,#133517,
#133518,#133519,#133520,#133521,#133522,#133523,#133524,#133525,#133526,
#133527,#133528,#133529,#133530,#133531,#133532,#133533,#133534,#133535,
#133536,#133537,#133538,#133539,#133540,#133541,#133542,#133543,#133544,
#133545,#133546),.UNSPECIFIED.,.F.,.F.,(4,3,3,3,3,3,3,3,3,3,3,3,3,3,3,3,
3,3,3,3,3,3,3,3,3,3,3,3,3,3,3,3,3,3,3,3,3,3,3,3,3,4),(91.1061869541041,
91.2043419644769,91.3024795334305,91.4006291648839,91.4988897541855,91.5972075103077,
91.6957053368612,91.7738402314764,91.8724383564801,91.9708961392567,92.0711187070294,
92.1693982647575,92.2676448438309,92.3658879268695,92.4675851155117,92.5659695289305,
92.6693231051843,92.7726766814382,92.8712748064418,92.9697325892184,93.0699551569911,
93.1682347147193,93.2664812937927,93.364724376831,93.4664215654733,93.564805978892,
93.668159555146,93.7715131314001,93.8701112564038,93.9685690391806,94.0687916069532,
94.1670711646813,94.2653177437548,94.3635608267933,94.4652580154355,94.5636424288542,
94.6669960051081,94.770349581362,94.8689185475044,94.9673651080001,95.0657083030471,
95.1638473408373),.UNSPECIFIED.);
#1310=B_SPLINE_CURVE_WITH_KNOTS('',3,(#133547,#133548,#133549,#133550,#133551,
#133552),.UNSPECIFIED.,.F.,.F.,(4,1,1,4),(88.8809435586522,89.7761673315526,
90.7750037815145,91.1061798195662),.UNSPECIFIED.);
#1311=B_SPLINE_CURVE_WITH_KNOTS('',3,(#133554,#133555,#133556,#133557,#133558,
#133559,#133560,#133561,#133562,#133563,#133564,#133565,#133566,#133567,
#133568,#133569,#133570,#133571,#133572,#133573,#133574,#133575,#133576,
#133577,#133578,#133579,#133580,#133581,#133582,#133583,#133584,#133585,
#133586,#133587,#133588,#133589,#133590,#133591,#133592,#133593,#133594,
#133595,#133596,#133597,#133598,#133599,#133600,#133601,#133602,#133603,
#133604,#133605,#133606,#133607,#133608,#133609,#133610,#133611,#133612,
#133613,#133614,#133615,#133616,#133617,#133618,#133619,#133620,#133621,
#133622,#133623,#133624,#133625,#133626),.UNSPECIFIED.,.F.,.F.,(4,3,3,3,
3,3,3,3,3,3,3,3,3,3,3,3,3,3,3,3,3,3,3,3,4),(88.8801389537999,88.9783987981197,
89.076767980697,89.1752004097067,89.2737927972633,89.311360599033,89.4099587240367,
89.5084165068134,89.6086390745861,89.7069186323142,89.8051652113876,89.9034082944261,
90.0051054830683,90.1034898964871,90.206843472741,90.3101970489949,90.409695787095,
90.5067185530535,90.6036495481492,90.70051989818,90.801936662084,90.8988156754799,
90.9957205549589,91.0927209416414,91.1061869537961),.UNSPECIFIED.);
#1312=B_SPLINE_CURVE_WITH_KNOTS('',3,(#133627,#133628,#133629,#133630,#133631,
#133632,#133633,#133634,#133635,#133636,#133637,#133638,#133639,#133640,
#133641,#133642,#133643,#133644,#133645,#133646,#133647,#133648,#133649,
#133650,#133651,#133652,#133653,#133654,#133655,#133656,#133657,#133658,
#133659,#133660,#133661,#133662,#133663,#133664,#133665,#133666,#133667,
#133668,#133669,#133670,#133671,#133672,#133673,#133674,#133675,#133676,
#133677,#133678,#133679,#133680,#133681,#133682,#133683,#133684,#133685,
#133686,#133687,#133688,#133689,#133690,#133691,#133692,#133693,#133694,
#133695,#133696,#133697,#133698,#133699,#133700,#133701,#133702,#133703,
#133704,#133705,#133706,#133707,#133708,#133709,#133710,#133711,#133712,
#133713,#133714,#133715,#133716,#133717,#133718,#133719,#133720,#133721,
#133722,#133723,#133724,#133725,#133726,#133727,#133728,#133729,#133730,
#133731,#133732,#133733,#133734,#133735,#133736,#133737,#133738,#133739,
#133740,#133741,#133742,#133743,#133744,#133745,#133746,#133747,#133748,
#133749,#133750),.UNSPECIFIED.,.F.,.F.,(4,3,3,3,3,3,3,3,3,3,3,3,3,3,3,3,
3,3,3,3,3,3,3,3,3,3,3,3,3,3,3,3,3,3,3,3,3,3,3,3,3,4),(91.1061869541041,
91.2465035596787,91.3090334989568,91.4076316239605,91.5060894067373,91.60631197451,
91.7045915322382,91.8028381113116,91.9010811943501,92.0027783829923,92.1011627964111,
92.2045163726649,92.3078699489186,92.4064680739223,92.5049258566991,92.6051484244717,
92.7034279821999,92.8016745612733,92.8999176443118,93.001614832954,93.0999992463728,
93.2033528226266,93.3067063988805,93.4053045238842,93.5037623066609,93.6039848744336,
93.7022644321618,93.8005110112352,93.8987540942737,94.0004512829158,94.0988356963346,
94.2021892725885,94.3055428488424,94.4041508037239,94.5025891903039,94.6009312472713,
94.6992065724891,94.7974446925389,94.8957159603349,94.9940021459913,95.0923959721904,
95.1629909577287),.UNSPECIFIED.);
#1313=B_SPLINE_CURVE_WITH_KNOTS('',3,(#133756,#133757,#133758,#133759,#133760,
#133761,#133762,#133763),.UNSPECIFIED.,.F.,.F.,(4,1,1,1,1,4),(97.3893797691262,
97.7668589312476,98.7656953812095,99.7645318311714,100.763368281133,101.445901991804),
 .UNSPECIFIED.);
#1314=B_SPLINE_CURVE_WITH_KNOTS('',3,(#133764,#133765,#133766,#133767,#133768,
#133769,#133770,#133771,#133772,#133773,#133774,#133775,#133776,#133777,
#133778,#133779,#133780,#133781,#133782,#133783,#133784,#133785,#133786,
#133787,#133788,#133789,#133790,#133791,#133792,#133793,#133794,#133795,
#133796,#133797,#133798,#133799,#133800,#133801,#133802,#133803,#133804,
#133805,#133806,#133807,#133808,#133809,#133810,#133811,#133812,#133813,
#133814,#133815,#133816,#133817,#133818,#133819,#133820,#133821,#133822,
#133823,#133824,#133825,#133826,#133827,#133828,#133829,#133830,#133831,
#133832,#133833,#133834,#133835,#133836),.UNSPECIFIED.,.F.,.F.,(4,3,3,3,
3,3,3,3,3,3,3,3,3,3,3,3,3,3,3,3,3,3,3,3,4),(95.1638473408373,95.2620943086999,
95.3603371625601,95.4625493797511,95.5609328931331,95.6593867503051,95.7579931826896,
95.7691860313238,95.8677841563276,95.9662419391048,96.0664645068774,96.1647440646056,
96.262990643679,96.3612337267177,96.4629309153597,96.5613153287784,96.664668905032,
96.7680224812857,96.8674993725788,96.9668292609828,97.0660403563902,97.1651524247997,
97.2642075332236,97.3632407686268,97.3893722612837),.UNSPECIFIED.);
#1315=B_SPLINE_CURVE_WITH_KNOTS('',3,(#133838,#133839,#133840,#133841,#133842,
#133843,#133844,#133845,#133846,#133847,#133848,#133849,#133850,#133851,
#133852,#133853,#133854,#133855,#133856,#133857,#133858,#133859,#133860,
#133861,#133862,#133863,#133864,#133865,#133866,#133867,#133868,#133869,
#133870,#133871,#133872,#133873,#133874,#133875,#133876,#133877,#133878,
#133879,#133880,#133881,#133882,#133883,#133884,#133885,#133886,#133887,
#133888,#133889,#133890,#133891,#133892,#133893,#133894,#133895,#133896,
#133897,#133898,#133899,#133900,#133901,#133902,#133903,#133904,#133905,
#133906,#133907),.UNSPECIFIED.,.F.,.F.,(4,3,3,3,3,3,3,3,3,3,3,3,3,3,3,3,
3,3,3,3,3,3,3,4),(95.1629909577287,95.2615808373963,95.3043792988043,95.402977423808,
95.5014352065847,95.6016577743574,95.6999373320855,95.7981839111589,95.8964269941974,
95.9981241828395,96.0965085962583,96.1998621725122,96.3032157487661,96.4018138737698,
96.5002716565466,96.6004942243192,96.6987737820474,96.7970203611207,96.8952634441592,
96.9969606328014,97.0953450462201,97.1986986224741,97.302052198728,97.3893722612837),
 .UNSPECIFIED.);
#1316=B_SPLINE_CURVE_WITH_KNOTS('',3,(#133908,#133909,#133910,#133911,#133912,
#133913,#133914,#133915),.UNSPECIFIED.,.F.,.F.,(4,1,1,1,1,4),(97.3893809711856,
98.3008886486899,99.2997250986518,100.298561548614,101.297397998576,101.447496653669),
 .UNSPECIFIED.);
#1317=B_SPLINE_CURVE_WITH_KNOTS('',3,(#133921,#133922,#133923,#133924,#133925,
#133926,#133927,#133928,#133929,#133930,#133931,#133932,#133933,#133934,
#133935,#133936,#133937,#133938,#133939,#133940,#133941,#133942,#133943,
#133944,#133945,#133946,#133947,#133948,#133949,#133950,#133951,#133952,
#133953,#133954,#133955,#133956,#133957,#133958,#133959,#133960,#133961,
#133962,#133963,#133964,#133965,#133966,#133967,#133968,#133969,#133970,
#133971,#133972,#133973,#133974,#133975,#133976,#133977,#133978,#133979,
#133980,#133981,#133982,#133983,#133984,#133985,#133986,#133987,#133988,
#133989,#133990,#133991,#133992,#133993,#133994,#133995,#133996,#133997,
#133998,#133999,#134000,#134001,#134002,#134003,#134004,#134005,#134006,
#134007,#134008,#134009,#134010,#134011,#134012,#134013,#134014,#134015,
#134016,#134017,#134018,#134019,#134020,#134021,#134022,#134023,#134024,
#134025,#134026,#134027,#134028,#134029,#134030,#134031,#134032,#134033,
#134034,#134035,#134036,#134037,#134038,#134039,#134040,#134041,#134042,
#134043,#134044),.UNSPECIFIED.,.F.,.F.,(4,3,3,3,3,3,3,3,3,3,3,3,3,3,3,3,
3,3,3,3,3,3,3,3,3,3,3,3,3,3,3,3,3,3,3,3,3,3,3,3,3,4),(103.672557568463,
103.759877631019,103.858475756023,103.956933538799,104.057156106572,104.1554356643,
104.253682243374,104.351925326412,104.453622515054,104.552006928473,104.655360504727,
104.758714080981,104.857312205985,104.955769988761,105.055992556534,105.154272114262,
105.252518693335,105.350761776374,105.452458965016,105.550843378435,105.654196954689,
105.757550530943,105.856148655947,105.954606438723,106.054829006496,106.153108564224,
106.251355143297,106.349598226336,106.451295414978,106.549679828397,106.65303340465,
106.756386980904,106.854986798947,106.953445809627,107.05178876834,107.150068003063,
107.248313037022,107.346553353054,107.444881222501,107.543251670454,107.641785788162,
107.72975655935),.UNSPECIFIED.);
#1318=B_SPLINE_CURVE_WITH_KNOTS('',3,(#134045,#134046,#134047,#134048,#134049,
#134050),.UNSPECIFIED.,.F.,.F.,(4,1,1,4),(101.445901991804,101.762204731095,
102.761041181057,103.67254885852),.UNSPECIFIED.);
#1319=B_SPLINE_CURVE_WITH_KNOTS('',3,(#134052,#134053,#134054,#134055,#134056,
#134057),.UNSPECIFIED.,.F.,.F.,(4,1,1,4),(101.447496653669,102.296234448537,
103.295070898499,103.672550060583),.UNSPECIFIED.);
#1320=B_SPLINE_CURVE_WITH_KNOTS('',3,(#134058,#134059,#134060,#134061,#134062,
#134063,#134064,#134065,#134066,#134067,#134068,#134069,#134070,#134071,
#134072,#134073,#134074,#134075,#134076,#134077,#134078,#134079,#134080,
#134081,#134082,#134083,#134084,#134085,#134086,#134087,#134088,#134089,
#134090,#134091,#134092,#134093,#134094,#134095,#134096,#134097,#134098,
#134099,#134100,#134101,#134102,#134103,#134104,#134105,#134106,#134107,
#134108,#134109,#134110,#134111,#134112,#134113,#134114,#134115,#134116,
#134117,#134118,#134119,#134120,#134121,#134122,#134123,#134124,#134125,
#134126,#134127,#134128,#134129,#134130,#134131,#134132,#134133,#134134,
#134135,#134136,#134137,#134138,#134139,#134140,#134141,#134142,#134143,
#134144,#134145,#134146,#134147,#134148,#134149,#134150,#134151,#134152,
#134153,#134154,#134155,#134156,#134157,#134158,#134159,#134160,#134161,
#134162,#134163,#134164,#134165,#134166,#134167,#134168,#134169,#134170,
#134171,#134172,#134173,#134174,#134175,#134176,#134177,#134178,#134179,
#134180,#134181,#134182,#134183,#134184),.UNSPECIFIED.,.F.,.F.,(4,3,3,3,
3,3,3,3,3,3,3,3,3,3,3,3,3,3,3,3,3,3,3,3,3,3,3,3,3,3,3,3,3,3,3,3,3,3,3,3,
3,3,4),(103.672557568463,103.771601702603,103.870660322484,103.96976131202,
104.06899945985,104.168318657834,104.267812431338,104.293907348461,104.392505473465,
104.490963256241,104.591185824014,104.689465381742,104.787711960816,104.885955043854,
104.987652232496,105.086036645915,105.189390222169,105.292743798423,105.391341923427,
105.489799706203,105.590022273976,105.688301831704,105.786548410778,105.884791493816,
105.986488682459,106.084873095877,106.188226672131,106.291580248385,106.390178373389,
106.488636156165,106.588858723938,106.687138281666,106.785384860739,106.883627943778,
106.98532513242,107.083709545839,107.187063122093,107.290416698347,107.38902306257,
107.48746439492,107.585810440424,107.684086111434,107.730086430664),
 .UNSPECIFIED.);
#1321=B_SPLINE_CURVE_WITH_KNOTS('',3,(#134190,#134191,#134192,#134193,#134194,
#134195,#134196,#134197,#134198,#134199,#134200,#134201,#134202,#134203,
#134204,#134205,#134206,#134207,#134208,#134209,#134210,#134211,#134212,
#134213,#134214,#134215,#134216,#134217,#134218,#134219,#134220,#134221,
#134222,#134223,#134224,#134225,#134226,#134227,#134228,#134229,#134230,
#134231,#134232,#134233,#134234,#134235,#134236,#134237,#134238,#134239,
#134240,#134241,#134242,#134243,#134244,#134245,#134246,#134247,#134248,
#134249,#134250,#134251,#134252,#134253,#134254,#134255,#134256,#134257,
#134258,#134259,#134260,#134261,#134262,#134263,#134264,#134265,#134266,
#134267,#134268,#134269,#134270,#134271,#134272,#134273,#134274,#134275,
#134276,#134277,#134278,#134279,#134280,#134281,#134282,#134283,#134284,
#134285,#134286,#134287,#134288,#134289,#134290,#134291,#134292,#134293,
#134294,#134295,#134296,#134297,#134298,#134299,#134300,#134301,#134302,
#134303,#134304,#134305,#134306,#134307,#134308,#134309,#134310,#134311,
#134312,#134313,#134314,#134315,#134316),.UNSPECIFIED.,.F.,.F.,(4,3,3,3,
3,3,3,3,3,3,3,3,3,3,3,3,3,3,3,3,3,3,3,3,3,3,3,3,3,3,3,3,3,3,3,3,3,3,3,3,
3,3,4),(109.955742875951,110.055241614051,110.152151423466,110.249014842069,
110.345862894414,110.447330365999,110.544300028994,110.641334438529,110.738518045248,
110.751732780752,110.850330905756,110.948788688532,111.049011256305,111.147290814033,
111.245537393106,111.343780476145,111.445477664787,111.543862078206,111.64721565446,
111.750569230714,111.849167355718,111.947625138495,112.047847706267,112.146127263995,
112.244373843069,112.342616926107,112.44431411475,112.542698528168,112.646052104422,
112.749405680676,112.84800380568,112.946461588456,113.046684156229,113.144963713957,
113.24321029303,113.341453376069,113.443150564711,113.54153497813,113.644888554384,
113.748242130638,113.846836224884,113.945278284704,114.013656815439),
 .UNSPECIFIED.);
#1322=B_SPLINE_CURVE_WITH_KNOTS('',3,(#134317,#134318,#134319,#134320,#134321,
#134322,#134323,#134324,#134325,#134326,#134327,#134328,#134329,#134330,
#134331,#134332,#134333,#134334,#134335,#134336,#134337,#134338,#134339,
#134340,#134341,#134342,#134343,#134344,#134345,#134346,#134347,#134348,
#134349,#134350,#134351,#134352,#134353,#134354,#134355,#134356,#134357,
#134358,#134359,#134360,#134361,#134362,#134363,#134364,#134365,#134366,
#134367,#134368,#134369,#134370,#134371,#134372,#134373,#134374,#134375,
#134376,#134377,#134378,#134379,#134380,#134381,#134382,#134383,#134384,
#134385,#134386),.UNSPECIFIED.,.F.,.F.,(4,3,3,3,3,3,3,3,3,3,3,3,3,3,3,3,
3,3,3,3,3,3,3,4),(107.72975655935,107.755223430866,107.85382155587,107.952279338646,
108.052501906419,108.150781464147,108.249028043221,108.347271126259,108.448968314901,
108.54735272832,108.650706304574,108.754059880828,108.852658005832,108.951115788608,
109.051338356381,109.149617914109,109.247864493183,109.346107576221,109.447804764863,
109.546189178282,109.649542754536,109.75289633079,109.893212936353,109.955742875643),
 .UNSPECIFIED.);
#1323=B_SPLINE_CURVE_WITH_KNOTS('',3,(#134388,#134389,#134390,#134391,#134392,
#134393,#134394,#134395,#134396,#134397,#134398,#134399,#134400,#134401,
#134402,#134403,#134404,#134405,#134406,#134407,#134408,#134409,#134410,
#134411,#134412,#134413,#134414,#134415,#134416,#134417,#134418,#134419,
#134420,#134421,#134422,#134423,#134424,#134425,#134426,#134427,#134428,
#134429,#134430,#134431,#134432,#134433,#134434,#134435,#134436,#134437,
#134438,#134439,#134440,#134441,#134442,#134443,#134444,#134445,#134446,
#134447,#134448,#134449,#134450,#134451,#134452,#134453,#134454,#134455,
#134456,#134457),.UNSPECIFIED.,.F.,.F.,(4,3,3,3,3,3,3,3,3,3,3,3,3,3,3,3,
3,3,3,3,3,3,3,4),(107.730086430664,107.828327794563,107.926578893471,108.024934180009,
108.123344704879,108.221924049223,108.289253148309,108.387851273313,108.486309056089,
108.586531623862,108.68481118159,108.783057760664,108.881300843702,108.982998032344,
109.081382445763,109.184736022017,109.288089598271,109.386591328536,109.484956309733,
109.583214317042,109.681399820025,109.779540599734,109.877698313766,109.955742875643),
 .UNSPECIFIED.);
#1324=B_SPLINE_CURVE_WITH_KNOTS('',3,(#134458,#134459,#134460,#134461,#134462,
#134463,#134464,#134465),.UNSPECIFIED.,.F.,.F.,(4,1,1,1,1,4),(109.95575001023,
110.286926048232,111.285762498194,112.284598948156,113.283435398118,114.012186952595),
 .UNSPECIFIED.);
#1325=B_SPLINE_CURVE_WITH_KNOTS('',3,(#134471,#134472,#134473,#134474,#134475,
#134476,#134477,#134478,#134479,#134480,#134481,#134482,#134483,#134484,
#134485,#134486,#134487,#134488,#134489,#134490,#134491,#134492,#134493,
#134494,#134495,#134496,#134497,#134498,#134499,#134500,#134501,#134502,
#134503,#134504,#134505,#134506,#134507,#134508,#134509,#134510,#134511,
#134512,#134513,#134514,#134515,#134516,#134517,#134518,#134519,#134520,
#134521,#134522,#134523,#134524,#134525,#134526,#134527,#134528,#134529,
#134530,#134531,#134532,#134533,#134534,#134535,#134536,#134537,#134538,
#134539,#134540,#134541,#134542,#134543,#134544,#134545,#134546,#134547,
#134548,#134549,#134550,#134551,#134552,#134553,#134554,#134555,#134556,
#134557,#134558,#134559,#134560,#134561,#134562,#134563,#134564,#134565,
#134566,#134567,#134568,#134569,#134570,#134571,#134572,#134573,#134574,
#134575,#134576,#134577,#134578,#134579,#134580,#134581,#134582,#134583,
#134584,#134585,#134586,#134587,#134588,#134589,#134590,#134591,#134592,
#134593,#134594),.UNSPECIFIED.,.F.,.F.,(4,3,3,3,3,3,3,3,3,3,3,3,3,3,3,3,
3,3,3,3,3,3,3,3,3,3,3,3,3,3,3,3,3,3,3,3,3,3,3,3,3,4),(116.238928182823,
116.341566510357,116.44447107289,116.547509821617,116.650828963887,116.744751480523,
116.843349605527,116.941807388303,117.042029956076,117.140309513804,117.238556092878,
117.336799175916,117.438496364558,117.536880777977,117.640234354231,117.743587930485,
117.842186055489,117.940643838265,118.040866406038,118.139145963766,118.23739254284,
118.335635625878,118.43733281452,118.535717227939,118.639070804193,118.742424380447,
118.841022505451,118.939480288227,119.039702856,119.137982413728,119.236228992802,
119.33447207584,119.436169264482,119.534553677901,119.637907254155,119.741260830409,
119.839851983057,119.938309194705,120.036651331114,120.134925920021,120.233176074197,
120.296103404723),.UNSPECIFIED.);
#1326=B_SPLINE_CURVE_WITH_KNOTS('',3,(#134595,#134596,#134597,#134598,#134599,
#134600,#134601,#134602,#134603,#134604,#134605,#134606,#134607,#134608,
#134609,#134610,#134611,#134612,#134613,#134614,#134615,#134616,#134617,
#134618,#134619,#134620,#134621,#134622,#134623,#134624,#134625,#134626,
#134627,#134628,#134629,#134630,#134631,#134632,#134633,#134634,#134635,
#134636,#134637,#134638,#134639,#134640,#134641,#134642,#134643,#134644,
#134645,#134646,#134647,#134648,#134649,#134650,#134651,#134652,#134653,
#134654,#134655,#134656,#134657,#134658,#134659,#134660,#134661,#134662,
#134663,#134664),.UNSPECIFIED.,.F.,.F.,(4,3,3,3,3,3,3,3,3,3,3,3,3,3,3,3,
3,3,3,3,3,3,3,4),(114.013656815439,114.111953393044,114.210207429762,114.308448417959,
114.406705828895,114.505071319279,114.603498058463,114.702086913916,114.747078580599,
114.845676705603,114.944134488379,115.044357056152,115.14263661388,115.240883192953,
115.339126275992,115.440823464634,115.539207878053,115.642561454307,115.745915030561,
115.84988875933,115.953561696348,116.057054365164,116.160309146371,116.238928182547),
 .UNSPECIFIED.);
#1327=B_SPLINE_CURVE_WITH_KNOTS('',3,(#134666,#134667,#134668,#134669,#134670,
#134671),.UNSPECIFIED.,.F.,.F.,(4,1,1,4),(114.012186952595,114.28227184808,
115.281108298042,116.238922797563),.UNSPECIFIED.);
#1328=B_SPLINE_CURVE_WITH_KNOTS('',3,(#134672,#134673,#134674,#134675,#134676,
#134677,#134678,#134679,#134680,#134681,#134682,#134683,#134684,#134685,
#134686,#134687,#134688,#134689,#134690,#134691,#134692,#134693,#134694,
#134695,#134696,#134697,#134698,#134699,#134700,#134701,#134702,#134703,
#134704,#134705,#134706,#134707,#134708,#134709,#134710,#134711,#134712,
#134713,#134714,#134715,#134716,#134717,#134718,#134719,#134720,#134721,
#134722,#134723,#134724,#134725,#134726,#134727,#134728,#134729,#134730,
#134731,#134732,#134733,#134734,#134735,#134736,#134737,#134738,#134739,
#134740,#134741,#134742,#134743,#134744,#134745,#134746,#134747,#134748,
#134749,#134750,#134751,#134752,#134753,#134754,#134755,#134756,#134757,
#134758,#134759,#134760,#134761,#134762,#134763,#134764,#134765,#134766,
#134767,#134768,#134769,#134770,#134771,#134772,#134773,#134774,#134775,
#134776,#134777,#134778,#134779,#134780,#134781,#134782,#134783,#134784,
#134785,#134786,#134787,#134788,#134789,#134790,#134791,#134792,#134793,
#134794,#134795,#134796,#134797,#134798),.UNSPECIFIED.,.F.,.F.,(4,3,3,3,
3,3,3,3,3,3,3,3,3,3,3,3,3,3,3,3,3,3,3,3,3,3,3,3,3,3,3,3,3,3,3,3,3,3,3,3,
3,3,4),(116.238928182823,116.279944748004,116.378542873008,116.477000655784,
116.577223223557,116.675502781285,116.773749360358,116.871992443397,116.973689632039,
117.072074045458,117.175427621712,117.278781197966,117.37737932297,117.475837105746,
117.576059673519,117.674339231247,117.77258581032,117.870828893359,117.972526082001,
118.07091049542,118.174264071673,118.277617647927,118.376215772931,118.474673555707,
118.57489612348,118.673175681208,118.771422260282,118.86966534332,118.971362531962,
119.069746945381,119.173100521635,119.276454097889,119.375052222893,119.47351000567,
119.573732573442,119.67201213117,119.770258710244,119.868501793282,119.970198981925,
120.068583395343,120.171936971597,120.275290547851,120.296396923363),
 .UNSPECIFIED.);
#1329=B_SPLINE_CURVE_WITH_KNOTS('',3,(#134804,#134805,#134806,#134807,#134808,
#134809,#134810,#134811),.UNSPECIFIED.,.F.,.F.,(4,1,1,1,1,4),(122.522113490002,
122.737770180294,123.736606630256,124.735443080218,125.73427953018,126.578666824116),
 .UNSPECIFIED.);
#1330=B_SPLINE_CURVE_WITH_KNOTS('',3,(#134812,#134813,#134814,#134815,#134816,
#134817,#134818,#134819,#134820,#134821,#134822,#134823,#134824,#134825,
#134826,#134827,#134828,#134829,#134830,#134831,#134832,#134833,#134834,
#134835,#134836,#134837,#134838,#134839,#134840,#134841,#134842,#134843,
#134844,#134845,#134846,#134847,#134848,#134849,#134850,#134851,#134852,
#134853,#134854,#134855,#134856,#134857,#134858,#134859,#134860,#134861,
#134862,#134863,#134864,#134865,#134866,#134867,#134868,#134869,#134870,
#134871,#134872,#134873,#134874,#134875,#134876,#134877,#134878,#134879,
#134880,#134881),.UNSPECIFIED.,.F.,.F.,(4,3,3,3,3,3,3,3,3,3,3,3,3,3,3,3,
3,3,3,3,3,3,3,4),(120.296103404723,120.394359158487,120.492722069624,120.591144783415,
120.689731197345,120.740097280371,120.838695405375,120.937153188151,121.037375755924,
121.135655313652,121.233901892726,121.332144975764,121.433842164406,121.532226577825,
121.635580154079,121.738933730333,121.836831200292,121.933909156543,122.030894120917,
122.127817176647,122.226391254986,122.323316910845,122.422715200424,122.522113490002),
 .UNSPECIFIED.);
#1331=B_SPLINE_CURVE_WITH_KNOTS('',3,(#134883,#134884,#134885,#134886,#134887,
#134888,#134889,#134890,#134891,#134892,#134893,#134894,#134895,#134896,
#134897,#134898,#134899,#134900,#134901,#134902,#134903,#134904,#134905,
#134906,#134907,#134908,#134909,#134910,#134911,#134912,#134913,#134914,
#134915,#134916,#134917,#134918,#134919,#134920,#134921,#134922,#134923,
#134924,#134925,#134926,#134927,#134928,#134929,#134930,#134931,#134932,
#134933,#134934,#134935,#134936,#134937,#134938,#134939,#134940,#134941,
#134942,#134943,#134944,#134945,#134946,#134947,#134948,#134949),
 .UNSPECIFIED.,.F.,.F.,(4,3,3,3,3,3,3,3,3,3,3,3,3,3,3,3,3,3,3,3,3,3,4),
(120.296396923363,120.394962257504,120.493394284,120.591721846097,120.689992664195,
120.788236250281,120.886482082457,120.98482755966,121.083221546878,121.181792233539,
121.274126997813,121.372725122817,121.471182905593,121.571405473366,121.669685031094,
121.767931610168,121.866174693206,121.967871881848,122.066256295267,122.169609871521,
122.272963447775,122.400857829823,122.522113389964),.UNSPECIFIED.);
#1332=B_SPLINE_CURVE_WITH_KNOTS('',3,(#134950,#134951,#134952,#134953,#134954,
#134955,#134956,#134957),.UNSPECIFIED.,.F.,.F.,(4,1,1,1,1,4),(122.522113490002,
123.271799897737,124.270636347699,125.26947279766,126.268309247622,126.580285757902),
 .UNSPECIFIED.);
#1333=B_SPLINE_CURVE_WITH_KNOTS('',3,(#134963,#134964,#134965,#134966,#134967,
#134968,#134969,#134970,#134971,#134972,#134973,#134974,#134975,#134976,
#134977,#134978,#134979,#134980,#134981,#134982,#134983,#134984,#134985,
#134986,#134987,#134988,#134989,#134990,#134991,#134992,#134993,#134994,
#134995,#134996,#134997,#134998,#134999,#135000,#135001,#135002,#135003,
#135004,#135005,#135006,#135007,#135008,#135009,#135010,#135011,#135012,
#135013,#135014,#135015,#135016,#135017,#135018,#135019,#135020,#135021,
#135022,#135023,#135024,#135025,#135026,#135027,#135028,#135029,#135030,
#135031,#135032,#135033,#135034,#135035,#135036,#135037,#135038,#135039,
#135040,#135041,#135042,#135043,#135044,#135045,#135046,#135047,#135048,
#135049,#135050,#135051,#135052,#135053,#135054,#135055,#135056,#135057,
#135058,#135059,#135060,#135061,#135062,#135063,#135064,#135065,#135066,
#135067,#135068,#135069,#135070,#135071,#135072,#135073,#135074,#135075,
#135076,#135077,#135078,#135079,#135080,#135081,#135082,#135083,#135084,
#135085,#135086,#135087,#135088,#135089),.UNSPECIFIED.,.F.,.F.,(4,3,3,3,
3,3,3,3,3,3,3,3,3,3,3,3,3,3,3,3,3,3,3,3,3,3,3,3,3,3,3,3,3,3,3,3,3,3,3,3,
3,3,4),(128.805298797182,128.902840431273,129.000250613517,129.097560812666,
129.194818343698,129.292053887497,129.389298094495,129.486642967568,129.584044330746,
129.68160592498,129.729625330028,129.828223455032,129.926681237808,130.026903805581,
130.125183363309,130.223429942382,130.321673025421,130.423370214063,130.521754627482,
130.625108203735,130.728461779989,130.827059904993,130.925517687769,131.025740255542,
131.12401981327,131.222266392343,131.320509475382,131.422206664024,131.520591077443,
131.623944653697,131.727298229951,131.825896354955,131.924354137732,132.024576705504,
132.122856263232,132.221102842306,132.319345925344,132.421043113987,132.519427527405,
132.622781103659,132.726134679913,132.824726637206,132.863178377909),
 .UNSPECIFIED.);
#1334=B_SPLINE_CURVE_WITH_KNOTS('',3,(#135090,#135091,#135092,#135093,#135094,
#135095,#135096),.UNSPECIFIED.,.F.,.F.,(4,1,1,1,4),(126.578666824116,126.733115980142,
127.731952430104,128.730788880066,128.805298797182),.UNSPECIFIED.);
#1335=B_SPLINE_CURVE_WITH_KNOTS('',3,(#135098,#135099,#135100,#135101,#135102,
#135103),.UNSPECIFIED.,.F.,.F.,(4,1,1,4),(126.580285757902,127.267145697584,
128.265982147546,128.805298797182),.UNSPECIFIED.);
#1336=B_SPLINE_CURVE_WITH_KNOTS('',3,(#135104,#135105,#135106,#135107,#135108,
#135109,#135110,#135111,#135112,#135113,#135114,#135115,#135116,#135117,
#135118,#135119,#135120,#135121,#135122,#135123,#135124,#135125,#135126,
#135127,#135128,#135129,#135130,#135131,#135132,#135133,#135134,#135135,
#135136,#135137,#135138,#135139,#135140,#135141,#135142,#135143,#135144,
#135145,#135146,#135147,#135148,#135149,#135150,#135151,#135152,#135153,
#135154,#135155,#135156,#135157,#135158,#135159,#135160,#135161,#135162,
#135163,#135164,#135165,#135166,#135167,#135168,#135169,#135170,#135171,
#135172,#135173,#135174,#135175,#135176,#135177,#135178,#135179,#135180,
#135181,#135182,#135183,#135184,#135185,#135186,#135187,#135188,#135189,
#135190,#135191,#135192,#135193,#135194,#135195,#135196,#135197,#135198,
#135199,#135200,#135201,#135202,#135203,#135204,#135205,#135206,#135207,
#135208,#135209,#135210,#135211,#135212,#135213,#135214,#135215,#135216,
#135217,#135218,#135219,#135220,#135221,#135222,#135223,#135224,#135225,
#135226,#135227),.UNSPECIFIED.,.F.,.F.,(4,3,3,3,3,3,3,3,3,3,3,3,3,3,3,3,
3,3,3,3,3,3,3,3,3,3,3,3,3,3,3,3,3,3,3,3,3,3,3,3,3,4),(128.805299011162,
128.910085619872,129.015255759152,129.120630109634,129.226318351048,129.264818597508,
129.363416722512,129.461874505289,129.562097073061,129.660376630789,129.758623209863,
129.856866292901,129.958563481543,130.056947894962,130.160301471216,130.26365504747,
130.362253172474,130.460710955251,130.560933523023,130.659213080752,130.757459659825,
130.855702742864,130.957399931506,131.055784344924,131.159137921178,131.262491497432,
131.361089622436,131.459547405212,131.559769972985,131.658049530713,131.756296109786,
131.854539192825,131.956236381467,132.054620794886,132.15797437114,132.261327947394,
132.3599137847,132.458366887935,132.559360488958,132.657635692185,132.759988492106,
132.862341292026),.UNSPECIFIED.);
#1337=B_SPLINE_CURVE_WITH_KNOTS('',3,(#135233,#135234,#135235,#135236,#135237,
#135238,#135239,#135240,#135241,#135242,#135243,#135244,#135245,#135246,
#135247,#135248,#135249,#135250,#135251,#135252,#135253,#135254,#135255,
#135256,#135257,#135258,#135259,#135260,#135261,#135262,#135263,#135264,
#135265,#135266,#135267,#135268,#135269,#135270,#135271,#135272,#135273,
#135274,#135275,#135276,#135277,#135278,#135279,#135280,#135281,#135282,
#135283,#135284,#135285,#135286,#135287,#135288,#135289,#135290,#135291,
#135292,#135293,#135294,#135295,#135296,#135297,#135298,#135299,#135300,
#135301,#135302,#135303,#135304,#135305,#135306,#135307,#135308,#135309,
#135310,#135311,#135312,#135313,#135314,#135315,#135316,#135317,#135318,
#135319,#135320,#135321,#135322,#135323,#135324,#135325,#135326,#135327,
#135328,#135329,#135330,#135331,#135332,#135333,#135334,#135335,#135336,
#135337,#135338,#135339,#135340,#135341,#135342,#135343,#135344,#135345,
#135346,#135347,#135348,#135349,#135350,#135351,#135352,#135353,#135354,
#135355,#135356,#135357,#135358,#135359),.UNSPECIFIED.,.F.,.F.,(4,3,3,3,
3,3,3,3,3,3,3,3,3,3,3,3,3,3,3,3,3,3,3,3,3,3,3,3,3,3,3,3,3,3,3,3,3,3,3,3,
3,3,4),(135.088484104361,135.187254556185,135.286029876603,135.384838499173,
135.483776463585,135.582788468007,135.681976179005,135.722644029799,135.821242154803,
135.91969993758,136.019922505352,136.11820206308,136.216448642154,136.314691725192,
136.416388913835,136.514773327253,136.618126903507,136.721480479761,136.820078604765,
136.918536387541,137.018758955314,137.117038513042,137.215285092115,137.313528175154,
137.415225363796,137.513609777215,137.616963353469,137.720316929723,137.818915054727,
137.917372837503,138.017595405276,138.115874963004,138.214121542077,138.312364625116,
138.414061813758,138.512446227177,138.61579980343,138.719153379684,138.817761602494,
138.916204188041,139.014551352306,139.112826031216,139.146050617851),
 .UNSPECIFIED.);
#1338=B_SPLINE_CURVE_WITH_KNOTS('',3,(#135360,#135361,#135362,#135363,#135364,
#135365,#135366,#135367,#135368,#135369,#135370,#135371,#135372,#135373,
#135374,#135375,#135376,#135377,#135378,#135379,#135380,#135381,#135382,
#135383,#135384,#135385,#135386,#135387,#135388,#135389,#135390,#135391,
#135392,#135393,#135394,#135395,#135396,#135397,#135398,#135399,#135400,
#135401,#135402,#135403,#135404,#135405,#135406,#135407,#135408,#135409,
#135410,#135411,#135412,#135413,#135414,#135415,#135416,#135417,#135418,
#135419,#135420,#135421,#135422,#135423,#135424,#135425,#135426,#135427,
#135428,#135429),.UNSPECIFIED.,.F.,.F.,(4,3,3,3,3,3,3,3,3,3,3,3,3,3,3,3,
3,3,3,3,3,3,3,4),(132.863178377909,132.961590295424,133.059905700764,133.1581695721,
133.256411413507,133.354660699864,133.453012805454,133.551418091656,133.649994565059,
133.724971129875,133.823569254879,133.922027037656,134.022249605428,134.120529163156,
134.21877574223,134.317018825268,134.41871601391,134.517100427329,134.620454003583,
134.723807579837,134.8363385207,134.948409000642,135.059693750754,135.088484104126),
 .UNSPECIFIED.);
#1339=B_SPLINE_CURVE_WITH_KNOTS('',3,(#135431,#135432,#135433,#135434,#135435,
#135436,#135437,#135438,#135439,#135440,#135441,#135442,#135443,#135444,
#135445,#135446,#135447,#135448,#135449,#135450,#135451,#135452,#135453,
#135454,#135455,#135456,#135457,#135458,#135459,#135460,#135461,#135462,
#135463,#135464,#135465,#135466,#135467,#135468,#135469,#135470,#135471,
#135472,#135473,#135474,#135475,#135476,#135477,#135478,#135479,#135480,
#135481,#135482,#135483,#135484,#135485,#135486,#135487,#135488,#135489,
#135490,#135491,#135492,#135493,#135494,#135495,#135496,#135497,#135498,
#135499,#135500),.UNSPECIFIED.,.F.,.F.,(4,3,3,3,3,3,3,3,3,3,3,3,3,3,3,3,
3,3,3,3,3,3,3,4),(132.862341292026,132.961797068358,133.060185474839,133.160174936097,
133.260164397355,133.358762522359,133.457220305135,133.557442872908,133.655722430636,
133.753969009709,133.852212092748,133.95390928139,134.052293694809,134.155647271063,
134.259000847317,134.356128675187,134.453094160804,134.549968416923,134.6467826177,
134.743567858739,134.84039997176,134.937256811786,135.034231214226,135.088484104361),
 .UNSPECIFIED.);
#1340=B_SPLINE_CURVE_WITH_KNOTS('',3,(#135501,#135502,#135503,#135504,#135505,
#135506,#135507,#135508),.UNSPECIFIED.,.F.,.F.,(4,1,1,1,1,4),(135.088484104361,
135.257837297279,136.256673747241,137.255510197203,138.254346647165,139.145213395082),
 .UNSPECIFIED.);
#1341=B_SPLINE_CURVE_WITH_KNOTS('',3,(#135514,#135515,#135516,#135517,#135518,
#135519,#135520,#135521,#135522,#135523,#135524,#135525,#135526,#135527,
#135528,#135529,#135530,#135531,#135532,#135533,#135534,#135535,#135536,
#135537,#135538,#135539,#135540,#135541,#135542,#135543,#135544,#135545,
#135546,#135547,#135548,#135549,#135550,#135551,#135552,#135553,#135554,
#135555,#135556,#135557,#135558,#135559,#135560,#135561,#135562,#135563,
#135564,#135565,#135566,#135567,#135568,#135569,#135570,#135571,#135572,
#135573,#135574,#135575,#135576,#135577,#135578,#135579,#135580,#135581,
#135582,#135583,#135584,#135585,#135586,#135587,#135588,#135589,#135590,
#135591,#135592,#135593,#135594,#135595,#135596,#135597,#135598,#135599,
#135600,#135601,#135602,#135603,#135604,#135605,#135606,#135607,#135608,
#135609,#135610,#135611,#135612,#135613,#135614,#135615,#135616,#135617,
#135618,#135619,#135620,#135621,#135622,#135623,#135624,#135625,#135626,
#135627,#135628,#135629,#135630,#135631,#135632,#135633,#135634,#135635,
#135636,#135637),.UNSPECIFIED.,.F.,.F.,(4,3,3,3,3,3,3,3,3,3,3,3,3,3,3,3,
3,3,3,3,3,3,3,3,3,3,3,3,3,3,3,3,3,3,3,3,3,3,3,3,3,4),(141.371669411768,
141.485016004535,141.600339367052,141.71566272957,141.814260854574,141.91271863735,
142.012941205123,142.111220762851,142.209467341925,142.307710424963,142.409407613605,
142.507792027024,142.611145603278,142.714499179532,142.813097304536,142.911555087312,
143.011777655085,143.110057212813,143.208303791887,143.306546874925,143.408244063567,
143.506628476986,143.60998205324,143.713335629494,143.811933754498,143.910391537275,
144.010614105047,144.108893662775,144.207140241849,144.305383324887,144.40708051353,
144.505464926948,144.608818503202,144.712172079456,144.810746601831,144.909191401419,
145.007536191859,145.105810581997,145.204060790383,145.302298022114,145.400579631078,
145.428467337346),.UNSPECIFIED.);
#1342=B_SPLINE_CURVE_WITH_KNOTS('',3,(#135638,#135639,#135640,#135641,#135642,
#135643,#135644,#135645,#135646,#135647,#135648,#135649,#135650,#135651,
#135652,#135653,#135654,#135655,#135656,#135657,#135658,#135659,#135660,
#135661,#135662,#135663,#135664,#135665,#135666,#135667,#135668,#135669,
#135670,#135671,#135672,#135673,#135674,#135675,#135676,#135677,#135678,
#135679,#135680,#135681,#135682,#135683,#135684,#135685,#135686,#135687,
#135688,#135689,#135690,#135691,#135692,#135693,#135694,#135695,#135696,
#135697,#135698,#135699,#135700,#135701,#135702,#135703,#135704,#135705,
#135706,#135707),.UNSPECIFIED.,.F.,.F.,(4,3,3,3,3,3,3,3,3,3,3,3,3,3,3,3,
3,3,3,3,3,3,3,4),(139.146050617851,139.244292880757,139.342541047598,139.440891102591,
139.539292953647,139.637867605968,139.717989829646,139.81658795465,139.915045737427,
140.015268305199,140.113547862927,140.211794442001,140.310037525039,140.411734713681,
140.5101191271,140.613472703354,140.716826279608,140.815569227393,140.914173010821,
141.012667061739,141.111081830931,141.209449097701,141.307822396312,141.371669411541),
 .UNSPECIFIED.);
#1343=B_SPLINE_CURVE_WITH_KNOTS('',3,(#135709,#135710,#135711,#135712,#135713,
#135714,#135715),.UNSPECIFIED.,.F.,.F.,(4,1,1,1,4),(139.145213395082,139.253183097127,
140.252019547089,141.25085599705,141.371669411541),.UNSPECIFIED.);
#1344=B_SPLINE_CURVE_WITH_KNOTS('',3,(#135716,#135717,#135718,#135719,#135720,
#135721,#135722,#135723,#135724,#135725,#135726,#135727,#135728,#135729,
#135730,#135731,#135732,#135733,#135734,#135735,#135736,#135737,#135738,
#135739,#135740,#135741,#135742,#135743,#135744,#135745,#135746,#135747,
#135748,#135749,#135750,#135751,#135752,#135753,#135754,#135755,#135756,
#135757,#135758,#135759,#135760,#135761,#135762,#135763,#135764,#135765,
#135766,#135767,#135768,#135769,#135770,#135771,#135772,#135773,#135774,
#135775,#135776,#135777,#135778,#135779,#135780,#135781,#135782,#135783,
#135784,#135785,#135786,#135787,#135788,#135789,#135790,#135791,#135792,
#135793,#135794,#135795,#135796,#135797,#135798,#135799,#135800,#135801,
#135802,#135803,#135804,#135805,#135806,#135807,#135808,#135809,#135810,
#135811,#135812,#135813,#135814,#135815,#135816,#135817,#135818,#135819,
#135820,#135821,#135822,#135823,#135824,#135825,#135826,#135827,#135828,
#135829,#135830,#135831,#135832,#135833,#135834,#135835,#135836,#135837,
#135838,#135839),.UNSPECIFIED.,.F.,.F.,(4,3,3,3,3,3,3,3,3,3,3,3,3,3,3,3,
3,3,3,3,3,3,3,3,3,3,3,3,3,3,3,3,3,3,3,3,3,3,3,3,3,4),(141.371669411541,
141.468831254161,141.566438903267,141.66339620349,141.760311911022,141.857216996242,
141.955335858935,142.052368429038,142.151030438025,142.249692447012,142.348290572016,
142.446748354792,142.546970922565,142.645250480293,142.743497059367,142.841740142405,
142.943437331047,143.041821744466,143.14517532072,143.248528896974,143.347127021978,
143.445584804754,143.545807372527,143.644086930255,143.742333509329,143.840576592367,
143.942273781009,144.040658194428,144.144011770682,144.247365346936,144.34596347194,
144.444421254716,144.544643822489,144.642923380217,144.741169959291,144.839413042329,
144.941110230971,145.03949464439,145.142848220644,145.246201796898,145.344774861155,
145.42960468327),.UNSPECIFIED.);
#1345=B_SPLINE_CURVE_WITH_KNOTS('',3,(#135845,#135846,#135847,#135848,#135849,
#135850,#135851,#135852,#135853),.UNSPECIFIED.,.F.,.F.,(4,1,1,1,1,1,4),
(147.65485471872,147.708681429341,148.707517879303,149.706354329265,150.705190779227,
151.704027229189,151.712252768111),.UNSPECIFIED.);
#1346=B_SPLINE_CURVE_WITH_KNOTS('',3,(#135854,#135855,#135856,#135857,#135858,
#135859,#135860,#135861,#135862,#135863,#135864,#135865,#135866,#135867,
#135868,#135869,#135870,#135871,#135872,#135873,#135874,#135875,#135876,
#135877,#135878,#135879,#135880,#135881,#135882,#135883,#135884,#135885,
#135886,#135887,#135888,#135889,#135890,#135891,#135892,#135893,#135894,
#135895,#135896,#135897,#135898,#135899,#135900,#135901,#135902,#135903,
#135904,#135905,#135906,#135907,#135908,#135909,#135910,#135911,#135912,
#135913,#135914,#135915,#135916,#135917,#135918,#135919,#135920,#135921,
#135922,#135923),.UNSPECIFIED.,.F.,.F.,(4,3,3,3,3,3,3,3,3,3,3,3,3,3,3,3,
3,3,3,3,3,3,3,4),(145.428467337346,145.526865630197,145.625438451516,145.711008529418,
145.809606654422,145.908064437198,146.008287004971,146.106566562699,146.204813141772,
146.303056224811,146.404753413453,146.503137826872,146.606491403125,146.709844979379,
146.807643480436,146.905302408374,147.002849316603,147.100335701354,147.197792033696,
147.295248746519,147.392798083501,147.490396206244,147.588155506493,147.65485471872),
 .UNSPECIFIED.);
#1347=B_SPLINE_CURVE_WITH_KNOTS('',3,(#135925,#135926,#135927,#135928,#135929,
#135930,#135931,#135932,#135933,#135934,#135935,#135936,#135937,#135938,
#135939,#135940,#135941,#135942,#135943,#135944,#135945,#135946,#135947,
#135948,#135949,#135950,#135951,#135952,#135953,#135954,#135955,#135956,
#135957,#135958,#135959,#135960,#135961,#135962,#135963,#135964,#135965,
#135966,#135967,#135968,#135969,#135970,#135971,#135972,#135973,#135974,
#135975,#135976,#135977,#135978,#135979,#135980,#135981,#135982,#135983,
#135984,#135985,#135986,#135987,#135988,#135989,#135990,#135991,#135992,
#135993,#135994),.UNSPECIFIED.,.F.,.F.,(4,3,3,3,3,3,3,3,3,3,3,3,3,3,3,3,
3,3,3,3,3,3,3,4),(145.42960468327,145.531533878718,145.629819454555,145.728068466941,
145.826310401823,145.924574729419,146.022950479282,146.121392844886,146.219991608955,
146.24503824686,146.343636371864,146.442094154641,146.542316722413,146.640596280141,
146.738842859215,146.837085942253,146.938783130896,147.037167544314,147.140521120568,
147.243874696822,147.352569174393,147.460952550047,147.568802109383,147.654854305396),
 .UNSPECIFIED.);
#1348=B_SPLINE_CURVE_WITH_KNOTS('',3,(#135995,#135996,#135997,#135998,#135999,
#136000,#136001,#136002),.UNSPECIFIED.,.F.,.F.,(4,1,1,1,1,4),(147.65485471872,
148.242711146784,149.241547596745,150.240384046707,151.239220496669,151.712342689598),
 .UNSPECIFIED.);
#1349=B_SPLINE_CURVE_WITH_KNOTS('',3,(#136008,#136009,#136010,#136011,#136012,
#136013,#136014,#136015,#136016,#136017,#136018,#136019,#136020,#136021,
#136022,#136023,#136024,#136025,#136026,#136027,#136028,#136029,#136030,
#136031,#136032,#136033,#136034,#136035,#136036,#136037,#136038,#136039,
#136040,#136041,#136042,#136043,#136044,#136045,#136046,#136047,#136048,
#136049,#136050,#136051,#136052,#136053,#136054,#136055,#136056,#136057,
#136058,#136059,#136060,#136061,#136062,#136063,#136064,#136065,#136066,
#136067,#136068,#136069,#136070,#136071,#136072,#136073,#136074,#136075,
#136076,#136077,#136078,#136079,#136080,#136081,#136082,#136083,#136084,
#136085,#136086,#136087,#136088,#136089,#136090,#136091,#136092,#136093,
#136094,#136095,#136096,#136097,#136098,#136099,#136100,#136101,#136102,
#136103,#136104,#136105,#136106,#136107,#136108,#136109,#136110,#136111,
#136112,#136113,#136114,#136115,#136116,#136117,#136118,#136119,#136120,
#136121,#136122,#136123,#136124,#136125,#136126,#136127,#136128,#136129,
#136130,#136131),.UNSPECIFIED.,.F.,.F.,(4,3,3,3,3,3,3,3,3,3,3,3,3,3,3,3,
3,3,3,3,3,3,3,3,3,3,3,3,3,3,3,3,3,3,3,3,3,3,3,3,3,4),(153.9380400259,154.035163898234,
154.132222574362,154.229246955324,154.326267897773,154.423381488606,154.520541056366,
154.617870832504,154.700536579074,154.799134704076,154.897592486852,154.997815054625,
155.096094612352,155.194341191424,155.292584274461,155.394281463105,155.492665876523,
155.596019452779,155.699373029036,155.797971154037,155.896428936811,155.996651504585,
156.09493106231,156.193177641381,156.291420724417,156.393117913062,156.491502326478,
156.594855902738,156.698209478998,156.796807604012,156.895265386799,156.995487954569,
157.093767512308,157.192014091391,157.29025717444,157.39195436307,157.490338776498,
157.593692352729,157.69704592896,157.79563212985,157.895770613718,157.995909097586),
 .UNSPECIFIED.);
#1350=B_SPLINE_CURVE_WITH_KNOTS('',3,(#136132,#136133,#136134,#136135,#136136,
#136137),.UNSPECIFIED.,.F.,.F.,(4,1,1,4),(151.712252768111,152.702863679151,
153.701700129113,153.938039726867),.UNSPECIFIED.);
#1351=B_SPLINE_CURVE_WITH_KNOTS('',3,(#136139,#136140,#136141,#136142,#136143,
#136144),.UNSPECIFIED.,.F.,.F.,(4,1,1,4),(151.712342689598,152.238056946631,
153.236893396593,153.9380400259),.UNSPECIFIED.);
#1352=B_SPLINE_CURVE_WITH_KNOTS('',3,(#136145,#136146,#136147,#136148,#136149,
#136150,#136151,#136152,#136153,#136154,#136155,#136156,#136157,#136158,
#136159,#136160,#136161,#136162,#136163,#136164,#136165,#136166,#136167,
#136168,#136169,#136170,#136171,#136172,#136173,#136174,#136175,#136176,
#136177,#136178,#136179,#136180,#136181,#136182,#136183,#136184,#136185,
#136186,#136187,#136188,#136189,#136190,#136191,#136192,#136193,#136194,
#136195,#136196,#136197,#136198,#136199,#136200,#136201,#136202,#136203,
#136204,#136205,#136206,#136207,#136208,#136209,#136210,#136211,#136212,
#136213,#136214,#136215,#136216,#136217,#136218,#136219,#136220,#136221,
#136222,#136223,#136224,#136225,#136226,#136227,#136228,#136229,#136230,
#136231,#136232,#136233,#136234,#136235,#136236,#136237,#136238,#136239,
#136240,#136241,#136242,#136243,#136244,#136245,#136246,#136247,#136248,
#136249,#136250,#136251,#136252,#136253,#136254,#136255,#136256,#136257,
#136258,#136259,#136260,#136261,#136262,#136263,#136264,#136265,#136266,
#136267,#136268),.UNSPECIFIED.,.F.,.F.,(4,3,3,3,3,3,3,3,3,3,3,3,3,3,3,3,
3,3,3,3,3,3,3,3,3,3,3,3,3,3,3,3,3,3,3,3,3,3,3,3,3,4),(153.938040202769,
154.056659980237,154.176963650994,154.235729846555,154.334327971559,154.432785754335,
154.533008322108,154.631287879836,154.729534458909,154.827777541948,154.92947473059,
155.027859144009,155.131212720263,155.234566296517,155.33316442152,155.431622204296,
155.531844772069,155.630124329797,155.72837090887,155.826613991908,155.928311180551,
156.026695593969,156.130049170224,156.233402746479,156.332000871484,156.430458654262,
156.530681222034,156.628960779764,156.727207358839,156.825450441879,156.927147630519,
157.025532043939,157.12888562019,157.23223919644,157.330809964381,157.429252216959,
157.527595662269,157.625869905304,157.724128943531,157.822375482211,157.920688283601,
157.994794042337),.UNSPECIFIED.);
#1353=B_SPLINE_CURVE_WITH_KNOTS('',3,(#136274,#136275,#136276,#136277,#136278,
#136279,#136280,#136281),.UNSPECIFIED.,.F.,.F.,(4,1,1,1,1,4),(160.221227414795,
160.693555278846,161.692391728808,162.691228178769,163.690064628731,164.278110089382),
 .UNSPECIFIED.);
#1354=B_SPLINE_CURVE_WITH_KNOTS('',3,(#136282,#136283,#136284,#136285,#136286,
#136287,#136288,#136289,#136290,#136291,#136292,#136293,#136294,#136295,
#136296,#136297,#136298,#136299,#136300,#136301,#136302,#136303,#136304,
#136305,#136306,#136307,#136308,#136309,#136310,#136311,#136312,#136313,
#136314,#136315,#136316,#136317,#136318,#136319,#136320,#136321,#136322,
#136323,#136324,#136325,#136326,#136327,#136328,#136329,#136330,#136331,
#136332,#136333,#136334,#136335,#136336,#136337,#136338,#136339,#136340,
#136341,#136342,#136343,#136344,#136345,#136346,#136347,#136348,#136349,
#136350,#136351),.UNSPECIFIED.,.F.,.F.,(4,3,3,3,3,3,3,3,3,3,3,3,3,3,3,3,
3,3,3,3,3,3,3,4),(157.995909097586,158.094187889713,158.192434178687,158.290677446715,
158.391978679767,158.490363789568,158.593123084245,158.695882378922,158.794480503912,
158.892938286675,158.993160854451,159.091440412165,159.189686991225,159.287930074249,
159.389627262908,159.488011676312,159.591365252598,159.694718828884,159.797216560019,
159.903218753284,160.005303397591,160.107256278835,160.209067828953,160.22122533308),
 .UNSPECIFIED.);
#1355=B_SPLINE_CURVE_WITH_KNOTS('',3,(#136353,#136354,#136355,#136356,#136357,
#136358,#136359,#136360,#136361,#136362,#136363,#136364,#136365,#136366,
#136367,#136368,#136369,#136370,#136371,#136372,#136373,#136374,#136375,
#136376,#136377,#136378,#136379,#136380,#136381,#136382,#136383,#136384,
#136385,#136386,#136387,#136388,#136389,#136390,#136391,#136392,#136393,
#136394,#136395,#136396,#136397,#136398,#136399,#136400,#136401,#136402,
#136403,#136404,#136405,#136406,#136407,#136408,#136409,#136410,#136411,
#136412,#136413,#136414,#136415,#136416,#136417,#136418,#136419,#136420,
#136421,#136422),.UNSPECIFIED.,.F.,.F.,(4,3,3,3,3,3,3,3,3,3,3,3,3,3,3,3,
3,3,3,3,3,3,3,4),(157.994794042337,158.093225162031,158.191816728715,158.231075646402,
158.329673771403,158.428131554177,158.528354121951,158.626633679676,158.724880258747,
158.823123341783,158.924820530428,159.023204943844,159.126558520104,159.229912096364,
159.328378576654,159.426704810661,159.526019875932,159.624169149678,159.722285836342,
159.820399593048,159.920606027993,160.018861091251,160.120043212039,160.221225332828),
 .UNSPECIFIED.);
#1356=B_SPLINE_CURVE_WITH_KNOTS('',3,(#136423,#136424,#136425,#136426,#136427,
#136428,#136429,#136430,#136431,#136432,#136433,#136434,#136435,#136436,
#136437,#136438,#136439,#136440,#136441,#136442,#136443,#136444,#136445,
#136446,#136447,#136448,#136449,#136450,#136451,#136452,#136453,#136454,
#136455,#136456,#136457,#136458,#136459,#136460,#136461,#136462,#136463,
#136464,#136465,#136466,#136467,#136468,#136469,#136470,#136471,#136472,
#136473,#136474,#136475,#136476,#136477,#136478,#136479,#136480,#136481,
#136482,#136483,#136484,#136485,#136486,#136487,#136488,#136489,#136490,
#136491,#136492,#136493,#136494,#136495,#136496,#136497,#136498,#136499,
#136500,#136501,#136502,#136503,#136504,#136505,#136506,#136507,#136508,
#136509,#136510,#136511,#136512,#136513,#136514,#136515,#136516,#136517,
#136518,#136519,#136520,#136521,#136522,#136523,#136524,#136525,#136526,
#136527,#136528,#136529,#136530,#136531,#136532,#136533,#136534,#136535,
#136536,#136537,#136538,#136539,#136540,#136541,#136542,#136543,#136544,
#136545,#136546,#136547,#136548,#136549),.UNSPECIFIED.,.F.,.F.,(4,3,3,3,
3,3,3,3,3,3,3,3,3,3,3,3,3,3,3,3,3,3,3,3,3,3,3,3,3,3,3,3,3,3,3,3,3,3,3,3,
3,3,4),(160.22122533308,160.228748546326,160.327346671318,160.425804454083,
160.526027021859,160.624306579575,160.722553158637,160.820796241664,160.92249343032,
161.020877843728,161.124231420008,161.227584996288,161.326183121278,161.424640904041,
161.524863471817,161.623143029531,161.72138960859,161.819632691614,161.921329880273,
162.019714293678,162.123067869964,162.22642144625,162.325019571326,162.423477354175,
162.52369992193,162.62197947973,162.720226058876,162.818469141986,162.920166330543,
163.018550744032,163.121904320122,163.225257896212,163.323856021116,163.422313803793,
163.522536371591,163.62081592922,163.719062508196,163.817305591138,163.919002779897,
164.017387193222,164.120740769698,164.224094346174,164.278857755076),
 .UNSPECIFIED.);
#1357=B_SPLINE_CURVE_WITH_KNOTS('',3,(#136555,#136556,#136557,#136558,#136559,
#136560,#136561,#136562,#136563,#136564,#136565,#136566,#136567,#136568,
#136569,#136570,#136571,#136572,#136573,#136574,#136575,#136576,#136577,
#136578,#136579,#136580,#136581,#136582,#136583,#136584,#136585,#136586,
#136587,#136588,#136589,#136590,#136591,#136592,#136593,#136594,#136595,
#136596,#136597,#136598,#136599,#136600,#136601,#136602,#136603,#136604,
#136605,#136606,#136607,#136608,#136609,#136610,#136611,#136612,#136613,
#136614,#136615,#136616,#136617,#136618,#136619,#136620,#136621,#136622,
#136623,#136624,#136625,#136626,#136627,#136628,#136629,#136630,#136631,
#136632,#136633,#136634,#136635,#136636,#136637,#136638,#136639,#136640,
#136641,#136642,#136643,#136644,#136645,#136646,#136647,#136648,#136649,
#136650,#136651,#136652,#136653,#136654,#136655,#136656,#136657,#136658,
#136659,#136660,#136661,#136662,#136663,#136664,#136665,#136666,#136667,
#136668,#136669,#136670,#136671,#136672,#136673,#136674,#136675,#136676,
#136677,#136678),.UNSPECIFIED.,.F.,.F.,(4,3,3,3,3,3,3,3,3,3,3,3,3,3,3,3,
3,3,3,3,3,3,3,3,3,3,3,3,3,3,3,3,3,3,3,3,3,3,3,3,3,4),(166.504410640259,
166.652910770048,166.686573978617,166.78517209724,166.883629873641,166.983852443008,
167.08213199442,167.180378567212,167.278621644013,167.380318840155,167.478703247507,
167.582056838043,167.685410428579,167.784008554557,167.882466338249,167.982688905786,
168.080968464281,168.179215044066,168.277458127759,168.379155315454,168.477539729381,
168.580893303961,168.684246878541,168.782845025208,168.88130282975,168.981525392094,
169.079804971676,169.17805157259,169.276294677425,169.377991840195,169.476376275083,
169.579729801793,169.683083328503,169.781689728101,169.88012748496,169.97846945026,
170.076745220522,170.174984321675,170.273261950963,170.371554713658,170.469968414811,
170.561255430934),.UNSPECIFIED.);
#1358=B_SPLINE_CURVE_WITH_KNOTS('',3,(#136679,#136680,#136681,#136682,#136683,
#136684),.UNSPECIFIED.,.F.,.F.,(4,1,1,4),(164.278110089382,164.688901078693,
165.687737528655,166.504405682607),.UNSPECIFIED.);
#1359=B_SPLINE_CURVE_WITH_KNOTS('',3,(#136686,#136687,#136688,#136689,#136690,
#136691,#136692,#136693,#136694,#136695,#136696,#136697,#136698,#136699,
#136700,#136701,#136702,#136703,#136704,#136705,#136706,#136707,#136708,
#136709,#136710,#136711,#136712,#136713,#136714,#136715,#136716,#136717,
#136718,#136719,#136720,#136721,#136722,#136723,#136724,#136725,#136726,
#136727,#136728,#136729,#136730,#136731,#136732,#136733,#136734,#136735,
#136736,#136737,#136738,#136739,#136740,#136741,#136742,#136743,#136744,
#136745,#136746,#136747,#136748,#136749,#136750,#136751,#136752,#136753,
#136754,#136755),.UNSPECIFIED.,.F.,.F.,(4,3,3,3,3,3,3,3,3,3,3,3,3,3,3,3,
3,3,3,3,3,3,3,4),(164.278857755076,164.377373896582,164.475767937975,164.574072811189,
164.672331019042,164.770572058965,164.868825403572,164.967184449585,165.065601043159,
165.164183843334,165.222930796135,165.321528921635,165.419986704909,165.520209272557,
165.618488830783,165.716735410353,165.814978493886,165.916675681939,166.015060095843,
166.11841367097,166.221767246097,166.344599874415,166.465474953167,166.504410639987),
 .UNSPECIFIED.);
#1360=B_SPLINE_CURVE_WITH_KNOTS('',3,(#136756,#136757,#136758,#136759,#136760,
#136761,#136762,#136763,#136764,#136765,#136766,#136767,#136768,#136769,
#136770,#136771,#136772,#136773,#136774,#136775,#136776,#136777,#136778,
#136779,#136780,#136781,#136782,#136783,#136784,#136785,#136786,#136787,
#136788,#136789,#136790,#136791,#136792,#136793,#136794,#136795,#136796,
#136797,#136798,#136799,#136800,#136801,#136802,#136803,#136804,#136805,
#136806,#136807,#136808,#136809,#136810,#136811,#136812,#136813,#136814,
#136815,#136816,#136817,#136818,#136819,#136820,#136821,#136822,#136823,
#136824,#136825,#136826,#136827,#136828,#136829,#136830,#136831,#136832,
#136833,#136834,#136835,#136836,#136837,#136838,#136839,#136840,#136841,
#136842,#136843,#136844,#136845,#136846,#136847,#136848,#136849,#136850,
#136851,#136852,#136853,#136854,#136855,#136856,#136857,#136858,#136859,
#136860,#136861,#136862,#136863,#136864,#136865,#136866,#136867,#136868,
#136869,#136870,#136871,#136872,#136873,#136874,#136875,#136876,#136877,
#136878,#136879,#136880,#136881,#136882),.UNSPECIFIED.,.F.,.F.,(4,3,3,3,
3,3,3,3,3,3,3,3,3,3,3,3,3,3,3,3,3,3,3,3,3,3,3,3,3,3,3,3,3,3,3,3,3,3,3,3,
3,3,4),(166.504410640259,166.6019131263,166.699371433808,166.79681599036,
166.894277201722,166.991846173226,167.089478292235,167.187269535436,167.220603696059,
167.319201820914,167.417659603534,167.517882171345,167.616161728897,167.714408307787,
167.812651390635,167.914348579482,168.012732992696,168.116086569359,168.219440146021,
168.318038274349,168.416496060462,168.516718627402,168.614998188473,168.713244770885,
168.811487857253,168.913185041936,169.011569458627,169.114923027305,169.218276595983,
169.316874714603,169.415332491002,169.51555506037,169.61383461178,169.71208118457,
169.810324261369,169.912021457513,170.010405864863,170.113759455404,170.217113045945,
170.315689889886,170.414143809236,170.512486666534,170.56219066747),
 .UNSPECIFIED.);
#1361=B_SPLINE_CURVE_WITH_KNOTS('',3,(#136888,#136889,#136890,#136891,#136892,
#136893,#136894,#136895,#136896,#136897,#136898,#136899,#136900,#136901,
#136902,#136903,#136904,#136905,#136906,#136907,#136908,#136909,#136910,
#136911,#136912,#136913,#136914,#136915,#136916,#136917,#136918,#136919,
#136920,#136921,#136922,#136923,#136924,#136925,#136926,#136927,#136928,
#136929,#136930,#136931,#136932,#136933,#136934,#136935,#136936,#136937,
#136938,#136939,#136940,#136941,#136942,#136943,#136944,#136945,#136946,
#136947,#136948,#136949,#136950,#136951,#136952,#136953,#136954,#136955,
#136956,#136957,#136958,#136959,#136960,#136961,#136962,#136963,#136964,
#136965,#136966,#136967,#136968,#136969,#136970,#136971,#136972,#136973,
#136974,#136975,#136976,#136977,#136978,#136979,#136980,#136981,#136982,
#136983,#136984,#136985,#136986,#136987,#136988,#136989,#136990,#136991,
#136992,#136993,#136994,#136995,#136996,#136997,#136998,#136999,#137000,
#137001,#137002,#137003,#137004,#137005,#137006,#137007,#137008,#137009,
#137010,#137011,#137012,#137013,#137014),.UNSPECIFIED.,.F.,.F.,(4,3,3,3,
3,3,3,3,3,3,3,3,3,3,3,3,3,3,3,3,3,3,3,3,3,3,3,3,3,3,3,3,3,3,3,3,3,3,3,3,
3,3,4),(172.787595947668,172.884841559506,172.984040005612,173.081071838667,
173.178059271087,173.275033215733,173.375882193887,173.472980628238,173.570144972561,
173.667458410759,173.67842912835,173.777027506202,173.875485539322,173.975708044196,
174.073987844422,174.172234662569,174.270477980966,174.372174880302,174.470559517526,
174.573912547919,174.677265578312,174.775864529236,174.874323143897,174.974545504444,
175.072825902575,175.171073323387,175.269317248384,175.371013443357,175.469398690653,
175.572750359463,175.676102028274,175.774697491594,175.873152609552,175.973375843138,
176.071652747408,176.169896682952,176.268137135791,176.369837471402,176.468219314363,
176.571578896299,176.674938478236,176.773518525278,176.845520762148),
 .UNSPECIFIED.);
#1362=B_SPLINE_CURVE_WITH_KNOTS('',3,(#137015,#137016,#137017,#137018,#137019,
#137020,#137021,#137022,#137023,#137024,#137025,#137026,#137027,#137028,
#137029,#137030,#137031,#137032,#137033,#137034,#137035,#137036,#137037,
#137038,#137039,#137040,#137041,#137042,#137043,#137044,#137045,#137046,
#137047,#137048,#137049,#137050,#137051,#137052,#137053,#137054,#137055,
#137056,#137057,#137058,#137059,#137060,#137061,#137062,#137063,#137064,
#137065,#137066,#137067,#137068,#137069,#137070,#137071,#137072,#137073,
#137074,#137075,#137076,#137077,#137078,#137079,#137080,#137081,#137082,
#137083,#137084),.UNSPECIFIED.,.F.,.F.,(4,3,3,3,3,3,3,3,3,3,3,3,3,3,3,3,
3,3,3,3,3,3,3,4),(170.561255430934,170.659855746347,170.681919778464,170.780517924844,
170.878975728609,170.979198291086,171.077477868714,171.175724467241,171.273967569265,
171.375664734055,171.474049165113,171.57740269677,171.680756228426,171.779354490085,
171.877812410303,171.978034943814,172.076314639908,172.174561357392,172.272804578702,
172.374501603624,172.472886153556,172.576239415972,172.679592678388,172.787595947439),
 .UNSPECIFIED.);
#1363=B_SPLINE_CURVE_WITH_KNOTS('',3,(#137086,#137087,#137088,#137089,#137090,
#137091,#137092,#137093,#137094,#137095,#137096,#137097,#137098,#137099,
#137100,#137101,#137102,#137103,#137104,#137105,#137106,#137107,#137108,
#137109,#137110,#137111,#137112,#137113,#137114,#137115,#137116,#137117,
#137118,#137119,#137120,#137121,#137122,#137123,#137124,#137125,#137126,
#137127,#137128,#137129,#137130,#137131,#137132,#137133,#137134,#137135,
#137136,#137137,#137138,#137139,#137140,#137141,#137142,#137143,#137144,
#137145,#137146,#137147,#137148,#137149,#137150,#137151,#137152,#137153,
#137154,#137155),.UNSPECIFIED.,.F.,.F.,(4,3,3,3,3,3,3,3,3,3,3,3,3,3,3,3,
3,3,3,3,3,3,3,4),(170.56219066747,170.660450504082,170.758691702558,170.856943736123,
170.95530060812,171.053713706999,171.152294500948,171.215949495907,171.314547642582,
171.413005447132,171.513228009474,171.611507589065,171.709754189987,171.807997294831,
171.909694457591,172.008078892487,172.111432419178,172.214785945869,172.315617765289,
172.416285943601,172.51678187547,172.617176498695,172.717484580153,172.787595947439),
 .UNSPECIFIED.);
#1364=B_SPLINE_CURVE_WITH_KNOTS('',3,(#137156,#137157,#137158,#137159,#137160,
#137161,#137162,#137163),.UNSPECIFIED.,.F.,.F.,(4,1,1,1,1,4),(172.787601414733,
173.21362239583,174.212458845792,175.211295295754,176.210131745716,176.844282066305),
 .UNSPECIFIED.);
#1365=B_SPLINE_CURVE_WITH_KNOTS('',3,(#137169,#137170,#137171,#137172,#137173,
#137174,#137175,#137176),.UNSPECIFIED.,.F.,.F.,(4,1,1,1,1,4),(179.070781254618,
179.671447828121,180.670284278083,181.669120728045,182.667957178007,183.128402534571),
 .UNSPECIFIED.);
#1366=B_SPLINE_CURVE_WITH_KNOTS('',3,(#137177,#137178,#137179,#137180,#137181,
#137182,#137183,#137184,#137185,#137186,#137187,#137188,#137189,#137190,
#137191,#137192,#137193,#137194,#137195,#137196,#137197,#137198,#137199,
#137200,#137201,#137202,#137203,#137204,#137205,#137206,#137207,#137208,
#137209,#137210,#137211,#137212,#137213,#137214,#137215,#137216,#137217,
#137218,#137219,#137220,#137221,#137222,#137223,#137224,#137225,#137226,
#137227,#137228,#137229,#137230,#137231,#137232,#137233,#137234,#137235,
#137236,#137237,#137238,#137239,#137240,#137241,#137242,#137243,#137244,
#137245,#137246),.UNSPECIFIED.,.F.,.F.,(4,3,3,3,3,3,3,3,3,3,3,3,3,3,3,3,
3,3,3,3,3,3,3,4),(176.845520762148,176.949052532905,177.047346579314,177.145600669623,
177.243844290299,177.342106909026,177.440479022331,177.538914695786,177.637509892069,
177.673774928198,177.772377752086,177.87084027796,177.971061665485,178.069346039597,
178.167597451746,178.265845378085,178.367536878104,178.465926110356,178.569268744257,
178.672611378159,178.782250156969,178.891545552981,179.000249474037,179.070781030164),
 .UNSPECIFIED.);
#1367=B_SPLINE_CURVE_WITH_KNOTS('',3,(#137248,#137249,#137250,#137251,#137252,
#137253),.UNSPECIFIED.,.F.,.F.,(4,1,1,4),(176.844282066305,177.208968195678,
178.20780464564,179.070781254618),.UNSPECIFIED.);
#1368=B_SPLINE_CURVE_WITH_KNOTS('',3,(#137254,#137255,#137256,#137257,#137258,
#137259,#137260,#137261),.UNSPECIFIED.,.F.,.F.,(4,1,1,1,1,4),(179.070781254618,
179.206641095602,180.205477545564,181.204313995525,182.203150445487,183.12768829285),
 .UNSPECIFIED.);
#1369=B_SPLINE_CURVE_WITH_KNOTS('',3,(#137267,#137268,#137269,#137270,#137271,
#137272,#137273,#137274),.UNSPECIFIED.,.F.,.F.,(4,1,1,1,1,4),(15.707963267949,
15.8622700343739,16.8611064843358,17.8599429342977,18.8587793842595,19.7647623489133),
 .UNSPECIFIED.);
#1370=B_SPLINE_CURVE_WITH_KNOTS('',3,(#137276,#137277,#137278,#137279,#137280,
#137281,#137282,#137283,#137284,#137285,#137286,#137287,#137288,#137289,
#137290,#137291,#137292,#137293,#137294,#137295,#137296,#137297,#137298,
#137299,#137300,#137301,#137302,#137303,#137304,#137305,#137306,#137307,
#137308,#137309,#137310,#137311,#137312,#137313,#137314,#137315,#137316,
#137317,#137318,#137319,#137320,#137321,#137322,#137323,#137324,#137325,
#137326,#137327,#137328,#137329,#137330,#137331,#137332,#137333),
 .UNSPECIFIED.,.F.,.F.,(4,3,3,3,3,3,3,3,3,3,3,3,3,3,3,3,3,3,3,4),(13.8757070305518,
13.9742335824856,14.0726198317922,14.1714715508697,14.2696802764454,14.3678558944916,
14.4660279816071,14.5653793823083,14.6636893819281,14.7635614831701,14.8634335844121,
14.9606976623845,15.0578044029831,15.1548229005499,15.2517842045426,15.3487192918042,
15.4457083561665,15.542724156859,15.6398692496992,15.707963267949),
 .UNSPECIFIED.);
#1371=B_SPLINE_CURVE_WITH_KNOTS('',3,(#137337,#137338,#137339,#137340,#137341),
 .UNSPECIFIED.,.F.,.F.,(4,1,4),(14.3986268518925,15.3974633018543,15.707963267949),
 .UNSPECIFIED.);
#1372=B_SPLINE_CURVE_WITH_KNOTS('',3,(#137342,#137343,#137344,#137345,#137346,
#137347,#137348,#137349),.UNSPECIFIED.,.F.,.F.,(4,1,1,1,1,4),(15.707963267949,
16.3962997518162,17.3951362017781,18.39397265174,19.3928091017018,19.7659327976564),
 .UNSPECIFIED.);
#1373=B_SPLINE_CURVE_WITH_KNOTS('',3,(#137355,#137356,#137357,#137358,#137359,
#137360,#137361,#137362),.UNSPECIFIED.,.F.,.F.,(4,1,1,1,1,4),(21.9911485751286,
22.854125184107,23.8529616340689,24.8517980840308,25.8506345339927,26.0493850849933),
 .UNSPECIFIED.);
#1374=B_SPLINE_CURVE_WITH_KNOTS('',3,(#137363,#137364,#137365,#137366,#137367,
#137368,#137369),.UNSPECIFIED.,.F.,.F.,(4,1,1,1,4),(19.7647623489133,19.8576158342214,
20.8564522841833,21.8552887341452,21.9911485751286),.UNSPECIFIED.);
#1375=B_SPLINE_CURVE_WITH_KNOTS('',3,(#137371,#137372,#137373,#137374,#137375,
#137376),.UNSPECIFIED.,.F.,.F.,(4,1,1,4),(19.7659327976564,20.3916455516637,
21.3904820016256,21.9911485751286),.UNSPECIFIED.);
#1376=B_SPLINE_CURVE_WITH_KNOTS('',3,(#137377,#137378,#137379,#137380,#137381,
#137382,#137383,#137384,#137385,#137386,#137387,#137388,#137389,#137390,
#137391,#137392,#137393,#137394,#137395,#137396,#137397,#137398,#137399,
#137400,#137401,#137402,#137403,#137404,#137405,#137406,#137407,#137408,
#137409,#137410,#137411,#137412,#137413,#137414,#137415,#137416,#137417,
#137418,#137419,#137420,#137421,#137422,#137423,#137424,#137425,#137426,
#137427,#137428,#137429,#137430,#137431,#137432,#137433,#137434,#137435,
#137436,#137437,#137438,#137439,#137440,#137441,#137442,#137443,#137444,
#137445,#137446,#137447,#137448,#137449,#137450,#137451,#137452,#137453,
#137454,#137455,#137456,#137457,#137458,#137459,#137460,#137461,#137462,
#137463,#137464,#137465,#137466,#137467,#137468,#137469,#137470,#137471,
#137472,#137473,#137474,#137475,#137476,#137477,#137478,#137479,#137480,
#137481,#137482,#137483,#137484,#137485,#137486,#137487,#137488,#137489,
#137490,#137491,#137492,#137493,#137494,#137495,#137496,#137497,#137498,
#137499,#137500),.UNSPECIFIED.,.F.,.F.,(4,3,3,3,3,3,3,3,3,3,3,3,3,3,3,3,
3,3,3,3,3,3,3,3,3,3,3,3,3,3,3,3,3,3,3,3,3,3,3,3,3,4),(21.9911487995803,
22.0999040794723,22.2090426325292,22.3187161977535,22.3893184515875,22.4879213239996,
22.5863838875782,22.6866052643246,22.7848896493686,22.8831410624577,22.9813889797561,
23.0830804602044,23.1814696586711,23.2848122801102,23.3881549015493,23.4867551943387,
23.5852151968621,23.6854372161932,23.7837191055958,23.8819680531268,23.9802135383925,
24.0819079916722,24.180294867534,24.2836431095226,24.3869913515112,24.4855869806887,
24.584042229485,24.6842654259835,24.7825423743751,24.8807863216562,24.9790267538739,
25.0807270157737,25.1791087577961,25.2824682796346,25.3858278014731,25.4844081036999,
25.582857277776,25.681205043018,25.7794880156384,25.8777310241197,25.9759959038317,
26.0480412469177),.UNSPECIFIED.);
#1377=B_SPLINE_CURVE_WITH_KNOTS('',3,(#137506,#137507,#137508,#137509,#137510,
#137511,#137512,#137513,#137514,#137515,#137516,#137517,#137518,#137519,
#137520,#137521,#137522,#137523,#137524,#137525,#137526,#137527,#137528,
#137529,#137530,#137531,#137532,#137533,#137534,#137535,#137536,#137537,
#137538,#137539,#137540,#137541,#137542,#137543,#137544,#137545,#137546,
#137547,#137548,#137549,#137550,#137551,#137552,#137553,#137554,#137555,
#137556,#137557,#137558,#137559,#137560,#137561,#137562,#137563,#137564,
#137565,#137566,#137567,#137568,#137569,#137570,#137571,#137572,#137573,
#137574,#137575,#137576,#137577,#137578,#137579,#137580,#137581,#137582,
#137583,#137584,#137585,#137586,#137587,#137588,#137589,#137590,#137591,
#137592,#137593,#137594,#137595,#137596,#137597,#137598,#137599,#137600,
#137601,#137602,#137603,#137604,#137605,#137606,#137607,#137608,#137609,
#137610,#137611,#137612,#137613,#137614,#137615,#137616,#137617,#137618,
#137619,#137620,#137621,#137622,#137623,#137624,#137625,#137626,#137627,
#137628,#137629),.UNSPECIFIED.,.F.,.F.,(4,3,3,3,3,3,3,3,3,3,3,3,3,3,3,3,
3,3,3,3,3,3,3,3,3,3,3,3,3,3,3,3,3,3,3,3,3,3,3,3,3,4),(28.2743338823082,
28.3746245106389,28.4749734038845,28.5754886320393,28.6760922702991,28.7769068624285,
28.8471438838783,28.9457420299505,29.0441998340411,29.144422396516,29.2427019760045,
29.3409485769573,29.4391916819654,29.5408888449341,29.6392732803233,29.7426268070817,
29.8459803338402,29.9445784592259,30.0430362424512,30.14325881012,30.2415383684582,
30.3397849482008,30.4380280319671,30.5397252199258,30.6381096342122,30.7414632090071,
30.844816783802,30.9434149029152,31.0418726796983,31.1420952489565,31.2403748004797,
31.3386213732828,31.4368644499936,31.5385616459362,31.6369460529487,31.7402996433563,
31.8436532337639,31.9422528703135,32.0406907036684,32.1390337581124,32.2373181769969,
32.331714806246),.UNSPECIFIED.);
#1378=B_SPLINE_CURVE_WITH_KNOTS('',3,(#137630,#137631,#137632,#137633,#137634,
#137635),.UNSPECIFIED.,.F.,.F.,(4,1,1,4),(26.0493850849933,26.8494709839545,
27.8483074339164,28.2743284148063),.UNSPECIFIED.);
#1379=B_SPLINE_CURVE_WITH_KNOTS('',3,(#137637,#137638,#137639,#137640,#137641,
#137642,#137643,#137644,#137645,#137646,#137647,#137648,#137649,#137650,
#137651,#137652,#137653,#137654,#137655,#137656,#137657,#137658,#137659,
#137660,#137661,#137662,#137663,#137664,#137665,#137666,#137667,#137668,
#137669,#137670,#137671,#137672,#137673,#137674,#137675,#137676,#137677,
#137678,#137679,#137680,#137681,#137682,#137683,#137684,#137685,#137686,
#137687,#137688,#137689,#137690,#137691,#137692,#137693,#137694,#137695,
#137696,#137697,#137698,#137699,#137700,#137701,#137702,#137703,#137704,
#137705,#137706,#137707,#137708,#137709),.UNSPECIFIED.,.F.,.F.,(4,3,3,3,
3,3,3,3,3,3,3,3,3,3,3,3,3,3,3,3,3,3,3,3,4),(26.0480412469177,26.1464094234963,
26.2448398572573,26.3434313033546,26.3846642514349,26.4832625887837,26.5817205899964,
26.6819431039214,26.7802228935228,26.8784697089924,26.976713032653,27.078409949839,
27.1767946120344,27.2801476567156,27.3835007013968,27.4808124357131,27.5800026165089,
27.6770619123618,27.7740624152157,27.8710350591815,27.971859764906,28.0689211638456,
28.1660361055543,28.2632831538734,28.2743338820794),.UNSPECIFIED.);
#1380=B_SPLINE_CURVE_WITH_KNOTS('',3,(#137710,#137711,#137712,#137713,#137714,
#137715,#137716,#137717,#137718,#137719,#137720,#137721,#137722,#137723,
#137724,#137725,#137726,#137727,#137728,#137729,#137730,#137731,#137732,
#137733,#137734,#137735,#137736,#137737,#137738,#137739,#137740,#137741,
#137742,#137743,#137744,#137745,#137746,#137747,#137748,#137749,#137750,
#137751,#137752,#137753,#137754,#137755,#137756,#137757,#137758,#137759,
#137760,#137761,#137762,#137763,#137764,#137765,#137766,#137767,#137768,
#137769,#137770,#137771,#137772,#137773,#137774,#137775,#137776,#137777,
#137778,#137779,#137780,#137781,#137782,#137783,#137784,#137785,#137786,
#137787,#137788,#137789,#137790,#137791,#137792,#137793,#137794,#137795,
#137796,#137797,#137798,#137799,#137800,#137801,#137802,#137803,#137804,
#137805,#137806,#137807,#137808,#137809,#137810,#137811,#137812,#137813,
#137814,#137815,#137816,#137817,#137818,#137819,#137820,#137821,#137822,
#137823,#137824,#137825,#137826,#137827,#137828,#137829,#137830,#137831,
#137832,#137833),.UNSPECIFIED.,.F.,.F.,(4,3,3,3,3,3,3,3,3,3,3,3,3,3,3,3,
3,3,3,3,3,3,3,3,3,3,3,3,3,3,3,3,3,3,3,3,3,3,3,3,3,4),(28.2743338823082,
28.3823371513587,28.480935409995,28.5793933278136,28.679615862002,28.7778955572416,
28.8761422744467,28.9743854960547,29.0760825223712,29.1744670740333,29.277820337677,
29.3811736013206,29.479771742719,29.5782295425603,29.6784521061506,29.7767316824742,
29.8749782806757,29.9732213833518,30.0749185503345,30.1733029844702,30.2766565178763,
30.3800100512824,30.4786081310924,30.5770658679195,30.6772884470851,30.7755679573387,
30.8738144884713,30.972057523165,31.0737547676848,31.1721391322403,31.2754928167423,
31.3788465012443,31.4774477473365,31.5759078066478,31.6742504130914,31.772528757936,
31.8707723648629,31.9690107165043,32.0673303009497,32.1656922449306,32.2642027658455,
32.3314303584533),.UNSPECIFIED.);
#1381=B_SPLINE_CURVE_WITH_KNOTS('',3,(#137839,#137840,#137841,#137842,#137843,
#137844,#137845,#137846,#137847,#137848,#137849,#137850,#137851,#137852,
#137853,#137854,#137855,#137856,#137857,#137858,#137859,#137860,#137861,
#137862,#137863,#137864,#137865,#137866,#137867,#137868,#137869,#137870,
#137871,#137872,#137873,#137874,#137875,#137876,#137877,#137878,#137879,
#137880,#137881,#137882,#137883,#137884,#137885,#137886,#137887,#137888,
#137889,#137890,#137891,#137892,#137893,#137894,#137895,#137896,#137897,
#137898,#137899,#137900,#137901,#137902,#137903,#137904,#137905,#137906,
#137907,#137908,#137909,#137910,#137911,#137912,#137913,#137914,#137915,
#137916,#137917,#137918,#137919,#137920,#137921,#137922,#137923,#137924,
#137925,#137926,#137927,#137928,#137929,#137930,#137931,#137932,#137933,
#137934,#137935,#137936,#137937,#137938,#137939,#137940,#137941,#137942,
#137943,#137944,#137945,#137946,#137947,#137948,#137949,#137950,#137951,
#137952,#137953,#137954,#137955,#137956,#137957,#137958,#137959,#137960,
#137961,#137962),.UNSPECIFIED.,.F.,.F.,(4,3,3,3,3,3,3,3,3,3,3,3,3,3,3,3,
3,3,3,3,3,3,3,3,3,3,3,3,3,3,3,3,3,3,3,3,3,3,3,3,3,4),(34.5575191897594,
34.6782345503606,34.8009387396023,34.8401625836495,34.9387607091287,35.0372184923872,
35.1374410600403,35.2357206182622,35.3339671978329,35.4322102813714,35.5339074694314,
35.6322918833521,35.7356454584817,35.8389990336114,35.9375971585481,36.0360549412581,
36.1362775090475,36.2345570667098,36.3328036457178,36.4310467286914,36.5327439174119,
36.631128330768,36.7344819071707,36.8378354835733,36.9364336084865,37.034891391171,
37.1351139589665,37.2333935165987,37.3316400955749,37.4298831785151,37.5315803672701,
37.629964780589,37.7333183570621,37.8366719335352,37.9352415778344,38.0336830992384,
38.1320262040958,38.2303004962045,38.3285627936546,38.4268127465241,38.5251372404893,
38.6142676701194),.UNSPECIFIED.);
#1382=B_SPLINE_CURVE_WITH_KNOTS('',3,(#137963,#137964,#137965,#137966,#137967,
#137968,#137969,#137970,#137971,#137972,#137973,#137974,#137975,#137976,
#137977,#137978,#137979,#137980,#137981,#137982,#137983,#137984,#137985,
#137986,#137987,#137988,#137989,#137990,#137991,#137992,#137993,#137994,
#137995,#137996,#137997,#137998,#137999,#138000,#138001,#138002,#138003,
#138004,#138005,#138006,#138007,#138008,#138009,#138010,#138011,#138012,
#138013,#138014,#138015,#138016,#138017,#138018,#138019,#138020,#138021,
#138022,#138023,#138024,#138025,#138026,#138027,#138028,#138029,#138030,
#138031,#138032,#138033,#138034,#138035),.UNSPECIFIED.,.F.,.F.,(4,3,3,3,
3,3,3,3,3,3,3,3,3,3,3,3,3,3,3,3,3,3,3,3,4),(32.331714806246,32.4299572859773,
32.5330903854144,32.6314723091546,32.7299238317575,32.8285286837753,32.8424896837258,
32.9410878085145,33.0395455910814,33.1397681589072,33.2380477164402,33.3362942953243,
33.4345373781797,33.5362345670567,33.6346189803101,33.7379725569989,33.8413261336877,
33.9390973941501,34.0367388270535,34.1342810926874,34.2317547370029,34.3292101035722,
34.4266554953253,34.5241539309012,34.5575191894878),.UNSPECIFIED.);
#1383=B_SPLINE_CURVE_WITH_KNOTS('',3,(#138037,#138038,#138039,#138040,#138041,
#138042,#138043,#138044,#138045,#138046,#138047,#138048,#138049,#138050,
#138051,#138052,#138053,#138054,#138055,#138056,#138057,#138058,#138059,
#138060,#138061,#138062,#138063,#138064,#138065,#138066,#138067,#138068,
#138069,#138070,#138071,#138072,#138073,#138074,#138075,#138076,#138077,
#138078,#138079,#138080,#138081,#138082,#138083,#138084,#138085,#138086,
#138087,#138088,#138089,#138090,#138091,#138092,#138093,#138094,#138095,
#138096,#138097,#138098,#138099,#138100,#138101,#138102,#138103,#138104,
#138105,#138106),.UNSPECIFIED.,.F.,.F.,(4,3,3,3,3,3,3,3,3,3,3,3,3,3,3,3,
3,3,3,3,3,3,3,4),(32.3314303584533,32.3776829512062,32.4762810765974,32.5747388598281,
32.6749614274956,32.7732409858386,32.8714875655859,32.9697306493566,33.0714278373095,
33.1698122515998,33.2731658263839,33.3765194011681,33.4751175203064,33.5735752971148,
33.6737978663667,33.7720774179164,33.8703239907463,33.9685670674843,34.0702642633957,
34.1686486704357,34.2720022607828,34.3753558511299,34.52385598093,34.5575191894878),
 .UNSPECIFIED.);
#1384=B_SPLINE_CURVE_WITH_KNOTS('',3,(#138107,#138108,#138109,#138110,#138111,
#138112,#138113,#138114),.UNSPECIFIED.,.F.,.F.,(4,1,1,1,1,4),(34.5575241472562,
35.3741923010918,36.3730287510537,37.3718652010156,38.3707016509774,38.6157831736331),
 .UNSPECIFIED.);
#1385=B_SPLINE_CURVE_WITH_KNOTS('',3,(#138120,#138121,#138122,#138123,#138124,
#138125,#138126,#138127,#138128,#138129,#138130,#138131,#138132,#138133,
#138134,#138135,#138136,#138137,#138138,#138139,#138140,#138141,#138142,
#138143,#138144,#138145,#138146,#138147,#138148,#138149,#138150,#138151,
#138152,#138153,#138154,#138155,#138156,#138157,#138158,#138159,#138160,
#138161,#138162,#138163,#138164,#138165,#138166,#138167,#138168,#138169,
#138170,#138171,#138172,#138173,#138174,#138175,#138176,#138177,#138178,
#138179,#138180,#138181,#138182,#138183,#138184,#138185,#138186,#138187,
#138188,#138189,#138190,#138191,#138192,#138193,#138194,#138195,#138196,
#138197,#138198,#138199,#138200,#138201,#138202,#138203,#138204,#138205,
#138206,#138207,#138208,#138209,#138210,#138211,#138212,#138213,#138214,
#138215,#138216,#138217,#138218,#138219,#138220,#138221,#138222,#138223,
#138224,#138225,#138226,#138227,#138228,#138229,#138230,#138231,#138232,
#138233,#138234,#138235,#138236,#138237,#138238,#138239,#138240,#138241,
#138242,#138243),.UNSPECIFIED.,.F.,.F.,(4,3,3,3,3,3,3,3,3,3,3,3,3,3,3,3,
3,3,3,3,3,3,3,3,3,3,3,3,3,3,3,3,3,3,3,3,3,3,3,3,3,4),(40.8407044969197,
40.93917053872,41.0374964280042,41.1368115911765,41.2349607512895,41.3330774110131,
41.4311912274065,41.5313978539005,41.6296531901077,41.7308354617452,41.8320177333826,
41.9306158583837,42.029073641158,42.1292962089313,42.2275757666567,42.3258223457274,
42.4240654287631,42.5257626174085,42.6241470308247,42.7275006070846,42.8308541833445,
42.929452308347,43.0279100911226,43.1281326588955,43.2264122166225,43.3246587956947,
43.4229018787318,43.5245990673755,43.622983480793,43.7263370570497,43.8296906333064,
43.9282887583114,44.0267465410897,44.126969108862,44.2252486665916,44.3234952456663,
44.4217383287063,44.5234355173468,44.621819930767,44.7251735070177,44.8285270832683,
44.8983979756935),.UNSPECIFIED.);
#1386=B_SPLINE_CURVE_WITH_KNOTS('',3,(#138244,#138245,#138246,#138247,#138248,
#138249,#138250,#138251,#138252,#138253,#138254,#138255,#138256,#138257,
#138258,#138259,#138260,#138261,#138262,#138263,#138264,#138265,#138266,
#138267,#138268,#138269,#138270,#138271,#138272,#138273,#138274,#138275,
#138276,#138277,#138278,#138279,#138280,#138281,#138282,#138283,#138284,
#138285,#138286,#138287,#138288,#138289,#138290,#138291,#138292,#138293,
#138294,#138295,#138296,#138297,#138298,#138299,#138300,#138301,#138302,
#138303,#138304,#138305,#138306,#138307,#138308,#138309,#138310,#138311,
#138312,#138313,#138314,#138315,#138316),.UNSPECIFIED.,.F.,.F.,(4,3,3,3,
3,3,3,3,3,3,3,3,3,3,3,3,3,3,3,3,3,3,3,3,4),(38.6142676701194,38.712710724348,
38.8113099394713,38.835508383497,38.9341065084864,39.0325642912488,39.132786859025,
39.2310664167387,39.3293129957977,39.4275560788219,39.5292532674811,39.6276376808858,
39.7309912571723,39.8343448334589,39.9329429584521,40.0314007412181,40.1316233089935,
40.2299028667104,40.3281494457725,40.4263925287994,40.5280897174548,40.6264741308618,
40.7298277071413,40.8331812834208,40.8407044966674),.UNSPECIFIED.);
#1387=B_SPLINE_CURVE_WITH_KNOTS('',3,(#138318,#138319,#138320,#138321,#138322,
#138323),.UNSPECIFIED.,.F.,.F.,(4,1,1,4),(38.6157831736331,39.3695381009393,
40.3683745509012,40.8407024149681),.UNSPECIFIED.);
#1388=B_SPLINE_CURVE_WITH_KNOTS('',3,(#138324,#138325,#138326,#138327,#138328,
#138329,#138330,#138331,#138332,#138333,#138334,#138335,#138336,#138337,
#138338,#138339,#138340,#138341,#138342,#138343,#138344,#138345,#138346,
#138347,#138348,#138349,#138350,#138351,#138352,#138353,#138354,#138355,
#138356,#138357,#138358,#138359,#138360,#138361,#138362,#138363,#138364,
#138365,#138366,#138367,#138368,#138369,#138370,#138371,#138372,#138373,
#138374,#138375,#138376,#138377,#138378,#138379,#138380,#138381,#138382,
#138383,#138384,#138385,#138386,#138387,#138388,#138389,#138390,#138391,
#138392,#138393,#138394,#138395,#138396,#138397,#138398,#138399,#138400,
#138401,#138402,#138403,#138404,#138405,#138406,#138407,#138408,#138409,
#138410,#138411,#138412,#138413,#138414,#138415,#138416,#138417,#138418,
#138419,#138420,#138421,#138422,#138423,#138424,#138425,#138426,#138427,
#138428,#138429,#138430,#138431,#138432,#138433,#138434,#138435,#138436,
#138437,#138438,#138439,#138440,#138441,#138442,#138443,#138444,#138445,
#138446,#138447,#138448,#138449,#138450),.UNSPECIFIED.,.F.,.F.,(4,3,3,3,
3,3,3,3,3,3,3,3,3,3,3,3,3,3,3,3,3,3,3,3,3,3,3,3,3,3,3,3,3,3,3,3,3,3,3,3,
3,3,4),(40.8407044966674,40.942531041993,41.0487010317105,41.1508691915792,
41.2531658485542,41.3556785603229,41.3672110008631,41.4658091258526,41.564266908615,
41.6644894763912,41.7627690341051,41.8610156131643,41.9592586961885,42.0609558848476,
42.1593402982524,42.2626938745386,42.3660474508249,42.4646455758181,42.5631033585841,
42.6633259263594,42.7616054840765,42.8598520631385,42.9580951461654,43.0597923348207,
43.1581767482279,43.2615303245073,43.3648839007868,43.4634820258002,43.5619398085867,
43.662162376357,43.7604419340952,43.8586885131789,43.9569315962276,44.0586287848578,
44.1570131982869,44.2603667745178,44.3637203507487,44.4623140220514,44.5607732131543,
44.6591152246742,44.7573894748763,44.8556332863477,44.8979423115668),
 .UNSPECIFIED.);
#1389=B_SPLINE_CURVE_WITH_KNOTS('',3,(#138456,#138457,#138458,#138459,#138460,
#138461,#138462,#138463),.UNSPECIFIED.,.F.,.F.,(4,1,1,1,1,4),(47.123889803847,
47.8250364331539,48.8238728831158,49.8227093330776,50.8215457830395,51.1819114106253),
 .UNSPECIFIED.);
#1390=B_SPLINE_CURVE_WITH_KNOTS('',3,(#138464,#138465,#138466,#138467,#138468,
#138469,#138470,#138471,#138472,#138473,#138474,#138475,#138476,#138477,
#138478,#138479,#138480,#138481,#138482,#138483,#138484,#138485,#138486,
#138487,#138488,#138489,#138490,#138491,#138492,#138493,#138494,#138495,
#138496,#138497,#138498,#138499,#138500,#138501,#138502,#138503,#138504,
#138505,#138506,#138507,#138508,#138509,#138510,#138511,#138512,#138513,
#138514,#138515,#138516,#138517,#138518,#138519,#138520,#138521,#138522,
#138523,#138524,#138525,#138526,#138527,#138528,#138529,#138530,#138531,
#138532,#138533),.UNSPECIFIED.,.F.,.F.,(4,3,3,3,3,3,3,3,3,3,3,3,3,3,3,3,
3,3,3,3,3,3,3,4),(44.8983979756935,44.9968932745396,45.0952715001835,45.1935673055801,
45.2918209691891,45.3900619829137,45.4883198179094,45.5866859593671,45.685113707856,
45.7837031830992,45.8273635332301,45.9259616582337,46.0244194410103,46.124642008783,
46.222921566511,46.3211681455842,46.4194112286227,46.521108417265,46.6194928306837,
46.7228464069379,46.826199983192,46.9466622822371,47.0654828012677,47.1238896269617),
 .UNSPECIFIED.);
#1391=B_SPLINE_CURVE_WITH_KNOTS('',3,(#138535,#138536,#138537,#138538,#138539,
#138540,#138541,#138542,#138543,#138544,#138545,#138546,#138547,#138548,
#138549,#138550,#138551,#138552,#138553,#138554,#138555,#138556,#138557,
#138558,#138559,#138560,#138561,#138562,#138563,#138564,#138565,#138566,
#138567,#138568,#138569,#138570,#138571,#138572,#138573,#138574,#138575,
#138576,#138577,#138578,#138579,#138580,#138581,#138582,#138583,#138584,
#138585,#138586,#138587,#138588,#138589,#138590,#138591,#138592,#138593,
#138594,#138595,#138596,#138597,#138598,#138599,#138600,#138601,#138602,
#138603,#138604),.UNSPECIFIED.,.F.,.F.,(4,3,3,3,3,3,3,3,3,3,3,3,3,3,3,3,
3,3,3,3,3,3,3,4),(44.8979423115668,44.996192512377,45.094546241849,45.1929542152813,
45.2915321477256,45.3625568007106,45.4611549257132,45.5596127084887,45.6598352762616,
45.7581148339886,45.8563614130607,45.9546044960983,46.0563016847418,46.1546860981594,
46.2580396744159,46.3613932506724,46.4587199838046,46.5559210250953,46.6530274701202,
46.750070296518,46.8471124553623,46.9441490048067,47.0412721236587,47.123889803847),
 .UNSPECIFIED.);
#1392=B_SPLINE_CURVE_WITH_KNOTS('',3,(#138605,#138606,#138607,#138608,#138609,
#138610,#138611,#138612),.UNSPECIFIED.,.F.,.F.,(4,1,1,1,1,4),(47.1238901027736,
47.3602297006343,48.3590661505962,49.3579026005581,50.3567390505199,51.1803882021177),
 .UNSPECIFIED.);
#1393=B_SPLINE_CURVE_WITH_KNOTS('',3,(#138618,#138619,#138620,#138621,#138622,
#138623,#138624,#138625,#138626,#138627,#138628,#138629,#138630,#138631,
#138632,#138633,#138634,#138635,#138636,#138637,#138638,#138639,#138640,
#138641,#138642,#138643,#138644,#138645,#138646,#138647,#138648,#138649,
#138650,#138651,#138652,#138653,#138654,#138655,#138656,#138657,#138658,
#138659,#138660,#138661,#138662,#138663,#138664,#138665,#138666,#138667,
#138668,#138669,#138670,#138671,#138672,#138673,#138674,#138675,#138676,
#138677,#138678,#138679,#138680,#138681,#138682,#138683,#138684,#138685,
#138686,#138687,#138688,#138689,#138690,#138691,#138692,#138693,#138694,
#138695,#138696,#138697,#138698,#138699,#138700,#138701,#138702,#138703,
#138704,#138705,#138706,#138707,#138708,#138709,#138710,#138711,#138712,
#138713,#138714,#138715,#138716,#138717,#138718,#138719,#138720,#138721,
#138722,#138723,#138724,#138725,#138726,#138727,#138728,#138729,#138730,
#138731,#138732,#138733,#138734,#138735,#138736,#138737,#138738,#138739,
#138740,#138741),.UNSPECIFIED.,.F.,.F.,(4,3,3,3,3,3,3,3,3,3,3,3,3,3,3,3,
3,3,3,3,3,3,3,3,3,3,3,3,3,3,3,3,3,3,3,3,3,3,3,3,3,4),(53.4070755243672,
53.5149520672774,53.6231638610727,53.7318758460234,53.8180551329251,53.9166532579288,
54.0151110407056,54.1153336084783,54.2136131662065,54.3118597452798,54.4101028283184,
54.5118000169605,54.6101844303793,54.7135380066332,54.816891582887,54.9154897078907,
55.0139474906675,55.1141700584402,55.2124496161683,55.3106961952417,55.4089392782802,
55.5106364669224,55.6090208803412,55.712374456595,55.8157280328489,55.9143261578525,
56.0127839406293,56.113006508402,56.2112860661301,56.3095326452035,56.407775728242,
56.5094729168842,56.607857330303,56.7112109065569,56.8145644828108,56.9131452274561,
57.0115945031595,57.1099420320482,57.208222759252,57.3064633876105,57.4047205556955,
57.463995981799),.UNSPECIFIED.);
#1394=B_SPLINE_CURVE_WITH_KNOTS('',3,(#138742,#138743,#138744,#138745,#138746,
#138747),.UNSPECIFIED.,.F.,.F.,(4,1,1,4),(51.1819114106253,51.8203822330014,
52.8192186829633,53.4070751110266),.UNSPECIFIED.);
#1395=B_SPLINE_CURVE_WITH_KNOTS('',3,(#138749,#138750,#138751,#138752,#138753,
#138754,#138755),.UNSPECIFIED.,.F.,.F.,(4,1,1,1,4),(51.1803882021177,51.3555755004818,
52.3544119504437,53.3532484004055,53.4070751110266),.UNSPECIFIED.);
#1396=B_SPLINE_CURVE_WITH_KNOTS('',3,(#138756,#138757,#138758,#138759,#138760,
#138761,#138762,#138763,#138764,#138765,#138766,#138767,#138768,#138769,
#138770,#138771,#138772,#138773,#138774,#138775,#138776,#138777,#138778,
#138779,#138780,#138781,#138782,#138783,#138784,#138785,#138786,#138787,
#138788,#138789,#138790,#138791,#138792,#138793,#138794,#138795,#138796,
#138797,#138798,#138799,#138800,#138801,#138802,#138803,#138804,#138805,
#138806,#138807,#138808,#138809,#138810,#138811,#138812,#138813,#138814,
#138815,#138816,#138817,#138818,#138819,#138820,#138821,#138822,#138823,
#138824,#138825,#138826,#138827,#138828,#138829,#138830,#138831,#138832,
#138833,#138834,#138835,#138836,#138837,#138838,#138839,#138840,#138841,
#138842,#138843,#138844,#138845,#138846,#138847,#138848,#138849,#138850,
#138851,#138852,#138853,#138854,#138855,#138856,#138857,#138858,#138859,
#138860,#138861,#138862,#138863,#138864,#138865,#138866,#138867,#138868,
#138869,#138870,#138871,#138872,#138873,#138874,#138875,#138876,#138877,
#138878,#138879,#138880,#138881,#138882),.UNSPECIFIED.,.F.,.F.,(4,3,3,3,
3,3,3,3,3,3,3,3,3,3,3,3,3,3,3,3,3,3,3,3,3,3,3,3,3,3,3,3,3,3,3,3,3,3,3,3,
3,3,4),(53.4070751110266,53.5048543854907,53.602498370777,53.7000367768844,
53.7975186210123,53.894974367796,53.9924344477701,54.0899931990352,54.1876041339862,
54.2853815723757,54.3520848503674,54.4506829753711,54.5491407581478,54.6493633259205,
54.7476428836486,54.8458894627221,54.9441325457605,55.0458297344027,55.1442141478216,
55.2475677240754,55.3509213003293,55.449519425333,55.5479772081098,55.6481997758825,
55.7464793336106,55.844725912684,55.9429689957225,56.0446661843647,56.1430505977836,
56.2464041740374,56.3497577502912,56.4483558752949,56.5468136580716,56.6470362258443,
56.7453157835724,56.8435623626458,56.9418054456842,57.0435026343264,57.1418870477453,
57.2452406239991,57.348594200253,57.4471969425917,57.4649113957591),
 .UNSPECIFIED.);
#1397=B_SPLINE_CURVE_WITH_KNOTS('',3,(#138888,#138889,#138890,#138891,#138892,
#138893,#138894,#138895),.UNSPECIFIED.,.F.,.F.,(4,1,1,1,1,4),(59.6902604182062,
59.8110738326964,60.8099102826583,61.8087467326201,62.807583182582,63.7472418296146),
 .UNSPECIFIED.);
#1398=B_SPLINE_CURVE_WITH_KNOTS('',3,(#138896,#138897,#138898,#138899,#138900,
#138901,#138902,#138903,#138904,#138905,#138906,#138907,#138908,#138909,
#138910,#138911,#138912,#138913,#138914,#138915,#138916,#138917,#138918,
#138919,#138920,#138921,#138922,#138923,#138924,#138925,#138926,#138927,
#138928,#138929,#138930,#138931,#138932,#138933,#138934,#138935,#138936,
#138937,#138938,#138939,#138940,#138941,#138942,#138943,#138944,#138945,
#138946,#138947,#138948,#138949,#138950,#138951,#138952,#138953,#138954,
#138955,#138956,#138957,#138958,#138959,#138960,#138961,#138962,#138963,
#138964,#138965),.UNSPECIFIED.,.F.,.F.,(4,3,3,3,3,3,3,3,3,3,3,3,3,3,3,3,
3,3,3,3,3,3,3,4),(57.463995981799,57.5623571755417,57.6607771836555,57.7593619848624,
57.8134009327726,57.9119990577763,58.010456840553,58.1106794083257,58.2089589660538,
58.3072055451272,58.4054486281657,58.5071458168079,58.6055302302267,58.7088838064806,
58.8122373827345,58.9094791608007,59.0070768179764,59.1040671063404,59.2009981633325,
59.2979009849178,59.3959908432399,59.4929780422907,59.5916192302484,59.6902604182062),
 .UNSPECIFIED.);
#1399=B_SPLINE_CURVE_WITH_KNOTS('',3,(#138967,#138968,#138969,#138970,#138971,
#138972,#138973,#138974,#138975,#138976,#138977,#138978,#138979,#138980,
#138981,#138982,#138983,#138984,#138985,#138986,#138987,#138988,#138989,
#138990,#138991,#138992,#138993,#138994,#138995,#138996,#138997,#138998,
#138999,#139000,#139001,#139002,#139003,#139004,#139005,#139006,#139007,
#139008,#139009,#139010,#139011,#139012,#139013,#139014,#139015,#139016,
#139017,#139018,#139019,#139020,#139021,#139022,#139023,#139024,#139025,
#139026,#139027,#139028,#139029,#139030,#139031,#139032,#139033),
 .UNSPECIFIED.,.F.,.F.,(4,3,3,3,3,3,3,3,3,3,3,3,3,3,3,3,3,3,3,3,3,3,4),
(57.4649113957591,57.5633474222124,57.6616774374564,57.7599497025695,57.8581937311631,
57.9564390020565,58.0547832942804,58.1531751948557,58.2517448810895,58.3474306502149,
58.4460287752185,58.5444865579955,58.6447091257682,58.7429886834964,58.8412352625699,
58.9394783456084,59.0411755342505,59.1395599476693,59.2429135239231,59.3462671001768,
59.4608829140302,59.5755716660047,59.6902604179793),.UNSPECIFIED.);
#1400=B_SPLINE_CURVE_WITH_KNOTS('',3,(#139034,#139035,#139036,#139037,#139038,
#139039,#139040,#139041,#139042,#139043,#139044,#139045,#139046,#139047,
#139048,#139049,#139050,#139051,#139052,#139053,#139054,#139055,#139056,
#139057,#139058,#139059,#139060,#139061,#139062,#139063,#139064,#139065,
#139066,#139067,#139068,#139069,#139070,#139071,#139072,#139073,#139074,
#139075,#139076,#139077,#139078,#139079,#139080,#139081,#139082,#139083,
#139084,#139085,#139086,#139087,#139088,#139089,#139090,#139091,#139092,
#139093,#139094,#139095,#139096,#139097,#139098,#139099,#139100,#139101,
#139102,#139103,#139104,#139105,#139106,#139107,#139108,#139109,#139110,
#139111,#139112,#139113,#139114,#139115,#139116,#139117,#139118,#139119,
#139120,#139121,#139122,#139123,#139124,#139125,#139126,#139127,#139128,
#139129,#139130,#139131,#139132,#139133,#139134,#139135,#139136,#139137,
#139138,#139139,#139140,#139141,#139142,#139143,#139144,#139145,#139146,
#139147,#139148,#139149,#139150,#139151,#139152,#139153,#139154,#139155,
#139156,#139157),.UNSPECIFIED.,.F.,.F.,(4,3,3,3,3,3,3,3,3,3,3,3,3,3,3,3,
3,3,3,3,3,3,3,3,3,3,3,3,3,3,3,3,3,3,3,3,3,3,3,3,3,4),(59.6902604182062,
59.7886341730559,59.8869985815967,59.985382791999,60.0838846667639,60.182449929213,
60.2811933482967,60.3451035501387,60.4437016751424,60.5421594579189,60.6423820256916,
60.7406615834198,60.8389081624931,60.9371512455316,61.0388484341738,61.1372328475927,
61.2405864238466,61.3439400001005,61.4425381251042,61.5409959078809,61.6412184756536,
61.7394980333817,61.8377446124552,61.9359876954936,62.0376848841358,62.1360692975546,
62.2394228738085,62.3427764500624,62.4413745750661,62.5398323578428,62.6400549256155,
62.7383344833436,62.836581062417,62.9348241454557,63.0365213340978,63.1349057475167,
63.2382593237705,63.3416129000243,63.4431811275695,63.5416227684091,63.644754289307,
63.7478858102049),.UNSPECIFIED.);
#1401=B_SPLINE_CURVE_WITH_KNOTS('',3,(#139163,#139164,#139165,#139166,#139167,
#139168,#139169,#139170,#139171,#139172,#139173,#139174,#139175,#139176,
#139177,#139178,#139179,#139180,#139181,#139182,#139183,#139184,#139185,
#139186,#139187,#139188,#139189,#139190,#139191,#139192,#139193,#139194,
#139195,#139196,#139197,#139198,#139199,#139200,#139201,#139202,#139203,
#139204,#139205,#139206,#139207,#139208,#139209,#139210,#139211,#139212,
#139213,#139214,#139215,#139216,#139217,#139218,#139219,#139220,#139221,
#139222,#139223,#139224,#139225,#139226,#139227,#139228,#139229,#139230,
#139231,#139232,#139233,#139234,#139235,#139236,#139237,#139238,#139239,
#139240,#139241,#139242,#139243,#139244,#139245,#139246,#139247,#139248,
#139249,#139250,#139251,#139252,#139253,#139254,#139255,#139256,#139257,
#139258,#139259,#139260,#139261,#139262,#139263,#139264,#139265,#139266,
#139267,#139268,#139269,#139270,#139271,#139272,#139273,#139274,#139275,
#139276,#139277,#139278,#139279,#139280,#139281,#139282,#139283,#139284,
#139285,#139286,#139287,#139288,#139289),.UNSPECIFIED.,.F.,.F.,(4,3,3,3,
3,3,3,3,3,3,3,3,3,3,3,3,3,3,3,3,3,3,3,3,3,3,3,3,3,3,3,3,3,3,3,3,3,3,3,3,
3,3,4),(65.9734457253857,66.0704340596177,66.1673127975357,66.2641328887558,
66.3609254267909,66.4577214670338,66.5546134226801,66.6515579893416,66.7486626585398,
66.8029289824295,66.9015271074333,66.9999848902101,67.1002074579827,67.1984870157109,
67.2967335947843,67.3949766778227,67.4966738664649,67.5950582798838,67.6984118561376,
67.8017654323914,67.9003635573951,67.998821340172,68.0990439079447,68.1973234656729,
68.2955700447463,68.3938131277847,68.4955103164269,68.5938947298456,68.6972483060994,
68.8006018823532,68.8992000073568,68.9976577901335,69.0978803579062,69.1961599156343,
69.2944064947076,69.3926495777462,69.4943467663884,69.5927311798071,69.6960847560611,
69.7994383323151,69.8980412657704,69.9964918402226,70.0313849607115),
 .UNSPECIFIED.);
#1402=B_SPLINE_CURVE_WITH_KNOTS('',3,(#139290,#139291,#139292,#139293,#139294,
#139295,#139296),.UNSPECIFIED.,.F.,.F.,(4,1,1,1,4),(63.7472418296146,63.8064196325439,
64.8052560825058,65.8040925324676,65.9734457253857),.UNSPECIFIED.);
#1403=B_SPLINE_CURVE_WITH_KNOTS('',3,(#139298,#139299,#139300,#139301,#139302,
#139303,#139304,#139305,#139306,#139307,#139308,#139309,#139310,#139311,
#139312,#139313,#139314,#139315,#139316,#139317,#139318,#139319,#139320,
#139321,#139322,#139323,#139324,#139325,#139326,#139327,#139328,#139329,
#139330,#139331,#139332,#139333,#139334,#139335,#139336,#139337,#139338,
#139339,#139340,#139341,#139342,#139343,#139344,#139345,#139346,#139347,
#139348,#139349,#139350,#139351,#139352,#139353,#139354,#139355,#139356,
#139357,#139358,#139359,#139360,#139361,#139362,#139363,#139364,#139365,
#139366,#139367),.UNSPECIFIED.,.F.,.F.,(4,3,3,3,3,3,3,3,3,3,3,3,3,3,3,3,
3,3,3,3,3,3,3,4),(63.7478858102049,63.8461305762455,63.9443750601028,64.0433936325736,
64.1417828323517,64.2411160911689,64.3404493499862,64.43904747499,64.5375052577664,
64.6377278255391,64.7360073832672,64.8342539623405,64.9324970453789,65.0341942340212,
65.1325786474399,65.235932223694,65.339285799948,65.4384637976082,65.53749807745,
65.6364173808604,65.7352455972605,65.8340208922139,65.932784900221,65.9734457253857),
 .UNSPECIFIED.);
#1404=B_SPLINE_CURVE_WITH_KNOTS('',3,(#139368,#139369,#139370,#139371,#139372,
#139373,#139374,#139375,#139376,#139377,#139378,#139379,#139380,#139381,
#139382,#139383,#139384,#139385,#139386,#139387,#139388,#139389,#139390,
#139391,#139392,#139393,#139394,#139395,#139396,#139397,#139398,#139399,
#139400,#139401,#139402,#139403,#139404,#139405,#139406,#139407,#139408,
#139409,#139410,#139411,#139412,#139413,#139414,#139415,#139416,#139417,
#139418,#139419,#139420,#139421,#139422,#139423,#139424,#139425,#139426,
#139427,#139428,#139429,#139430,#139431,#139432,#139433,#139434,#139435,
#139436,#139437,#139438,#139439,#139440,#139441,#139442,#139443,#139444,
#139445,#139446,#139447,#139448,#139449,#139450,#139451,#139452,#139453,
#139454,#139455,#139456,#139457,#139458,#139459,#139460,#139461,#139462,
#139463,#139464,#139465,#139466,#139467,#139468,#139469,#139470,#139471,
#139472,#139473,#139474,#139475,#139476,#139477,#139478,#139479,#139480,
#139481,#139482,#139483,#139484,#139485,#139486,#139487,#139488,#139489,
#139490,#139491),.UNSPECIFIED.,.F.,.F.,(4,3,3,3,3,3,3,3,3,3,3,3,3,3,3,3,
3,3,3,3,3,3,3,3,3,3,3,3,3,3,3,3,3,3,3,3,3,3,3,3,3,4),(65.9734457256204,
66.0848798050741,66.1968635637043,66.309495782683,66.3381222499099,66.4367203749136,
66.5351781576904,66.6354007254631,66.7336802831912,66.8319268622646,66.9301699453032,
67.0318671339454,67.1302515473642,67.233605123618,67.3369586998718,67.4355568248755,
67.5340146076523,67.6342371754249,67.7325167331531,67.8307633122265,67.929006395265,
68.0307035839072,68.129087997326,68.2324415735798,68.3357951498337,68.4343932748374,
68.5328510576141,68.6330736253868,68.7313531831149,68.8295997621883,68.9278428452268,
69.029540033869,69.1279244472878,69.2312780235416,69.3346315997955,69.4332079436462,
69.5316540255,69.6299995615592,69.7300684041619,69.8283147746266,69.9292948532983,
70.03027493197),.UNSPECIFIED.);
#1405=B_SPLINE_CURVE_WITH_KNOTS('',3,(#139497,#139498,#139499,#139500,#139501,
#139502,#139503,#139504),.UNSPECIFIED.,.F.,.F.,(4,1,1,1,1,4),(72.2566310325654,
72.7959476822007,73.7947841321626,74.7936205821245,75.7924570320864,76.313857464374),
 .UNSPECIFIED.);
#1406=B_SPLINE_CURVE_WITH_KNOTS('',3,(#139505,#139506,#139507,#139508,#139509,
#139510,#139511,#139512,#139513,#139514,#139515,#139516,#139517,#139518,
#139519,#139520,#139521,#139522,#139523,#139524,#139525,#139526,#139527,
#139528,#139529,#139530,#139531,#139532,#139533,#139534,#139535,#139536,
#139537,#139538,#139539,#139540,#139541,#139542,#139543,#139544,#139545,
#139546,#139547,#139548,#139549,#139550,#139551,#139552,#139553,#139554,
#139555,#139556,#139557,#139558,#139559,#139560,#139561,#139562,#139563,
#139564,#139565,#139566,#139567,#139568,#139569,#139570,#139571,#139572,
#139573,#139574),.UNSPECIFIED.,.F.,.F.,(4,3,3,3,3,3,3,3,3,3,3,3,3,3,3,3,
3,3,3,3,3,3,3,4),(70.0313849607115,70.1297027503805,70.2279679525357,70.3262100727843,
70.4244585865919,70.5228092852778,70.6212122199263,70.7197874411937,70.798274782277,
70.8968729072807,70.9953306900577,71.0955532578304,71.1938328155586,71.292079394632,
71.3903224776701,71.4920196663123,71.5904040797311,71.693757655985,71.7971112322389,
71.9028340905511,72.0081993817375,72.1133399321499,72.2181701837239,72.2566308185779),
 .UNSPECIFIED.);
#1407=B_SPLINE_CURVE_WITH_KNOTS('',3,(#139576,#139577,#139578,#139579,#139580,
#139581,#139582,#139583,#139584,#139585,#139586,#139587,#139588,#139589,
#139590,#139591,#139592,#139593,#139594,#139595,#139596,#139597,#139598,
#139599,#139600,#139601,#139602,#139603,#139604,#139605,#139606,#139607,
#139608,#139609,#139610,#139611,#139612,#139613,#139614,#139615,#139616,
#139617,#139618,#139619,#139620,#139621,#139622,#139623,#139624,#139625,
#139626,#139627,#139628,#139629,#139630,#139631,#139632,#139633,#139634,
#139635,#139636,#139637,#139638,#139639,#139640,#139641,#139642,#139643,
#139644,#139645),.UNSPECIFIED.,.F.,.F.,(4,3,3,3,3,3,3,3,3,3,3,3,3,3,3,3,
3,3,3,3,3,3,3,4),(70.03027493197,70.1286604602104,70.2310642549839,70.3334680497574,
70.4320661747611,70.5305239575378,70.6307465253105,70.7290260830386,70.827272662112,
70.9255157451505,71.0272129337927,71.1255973472115,71.2289509234654,71.3323044997193,
71.4298807240688,71.5273176349421,71.6246428433669,71.721908115062,71.8191441424516,
71.9163815796695,72.013708783522,72.1110862397604,72.2086145464311,72.2566310325654),
 .UNSPECIFIED.);
#1408=B_SPLINE_CURVE_WITH_KNOTS('',3,(#139646,#139647,#139648,#139649,#139650,
#139651,#139652,#139653),.UNSPECIFIED.,.F.,.F.,(4,1,1,1,1,4),(72.2566310325654,
72.3311409496812,73.329977399643,74.3288138496049,75.3276502995668,76.3138964218534),
 .UNSPECIFIED.);
#1409=B_SPLINE_CURVE_WITH_KNOTS('',3,(#139659,#139660,#139661,#139662,#139663,
#139664,#139665,#139666,#139667,#139668,#139669,#139670,#139671,#139672,
#139673,#139674,#139675,#139676,#139677,#139678,#139679,#139680,#139681,
#139682,#139683,#139684,#139685,#139686,#139687,#139688,#139689,#139690,
#139691,#139692,#139693,#139694,#139695,#139696,#139697,#139698,#139699,
#139700,#139701,#139702,#139703,#139704,#139705,#139706,#139707,#139708,
#139709,#139710,#139711,#139712,#139713,#139714,#139715,#139716,#139717,
#139718,#139719,#139720,#139721,#139722,#139723,#139724,#139725,#139726,
#139727,#139728,#139729,#139730,#139731,#139732,#139733,#139734,#139735,
#139736,#139737,#139738,#139739,#139740,#139741,#139742,#139743,#139744,
#139745,#139746,#139747,#139748,#139749,#139750,#139751,#139752,#139753,
#139754,#139755,#139756,#139757,#139758,#139759,#139760,#139761,#139762,
#139763,#139764,#139765,#139766,#139767,#139768,#139769,#139770,#139771,
#139772,#139773,#139774,#139775,#139776,#139777,#139778,#139779,#139780,
#139781,#139782),.UNSPECIFIED.,.F.,.F.,(4,3,3,3,3,3,3,3,3,3,3,3,3,3,3,3,
3,3,3,3,3,3,3,3,3,3,3,3,3,3,3,3,3,3,3,3,3,3,3,3,3,4),(78.5398164398184,
78.6677108218573,78.788966381972,78.8875645069757,78.9860222897525,79.0862448575251,
79.1845244152533,79.2827709943267,79.3810140773652,79.4827112660074,79.5810956794262,
79.6844492556801,79.7878028319339,79.8864009569376,79.9848587397143,80.085081307487,
80.1833608652152,80.2816074442885,80.379850527327,80.4815477159692,80.579932129388,
80.6832857056419,80.7866392818957,80.8852374068994,80.9836951896762,81.0839177574488,
81.182197315177,81.2804438942504,81.3786869772889,81.4803841659311,81.5787685793499,
81.6821221556037,81.7854757318576,81.8868624848001,81.9852993438176,82.0836395049705,
82.1819125670158,82.2801480566582,82.3784063425592,82.4766798090168,82.5750348041364,
82.5965697553975),.UNSPECIFIED.);
#1410=B_SPLINE_CURVE_WITH_KNOTS('',3,(#139783,#139784,#139785,#139786,#139787,
#139788),.UNSPECIFIED.,.F.,.F.,(4,1,1,4),(76.313857464374,76.7912934820482,
77.7901299320101,78.539816339745),.UNSPECIFIED.);
#1411=B_SPLINE_CURVE_WITH_KNOTS('',3,(#139790,#139791,#139792,#139793,#139794,
#139795,#139796),.UNSPECIFIED.,.F.,.F.,(4,1,1,1,4),(76.3138964218534,76.3264867495287,
77.3253231994905,78.3241596494524,78.539816339745),.UNSPECIFIED.);
#1412=B_SPLINE_CURVE_WITH_KNOTS('',3,(#139797,#139798,#139799,#139800,#139801,
#139802,#139803,#139804,#139805,#139806,#139807,#139808,#139809,#139810,
#139811,#139812,#139813,#139814,#139815,#139816,#139817,#139818,#139819,
#139820,#139821,#139822,#139823,#139824,#139825,#139826,#139827,#139828,
#139829,#139830,#139831,#139832,#139833,#139834,#139835,#139836,#139837,
#139838,#139839,#139840,#139841,#139842,#139843,#139844,#139845,#139846,
#139847,#139848,#139849,#139850,#139851,#139852,#139853,#139854,#139855,
#139856,#139857,#139858,#139859,#139860,#139861,#139862,#139863,#139864,
#139865,#139866,#139867,#139868,#139869,#139870,#139871,#139872,#139873,
#139874,#139875,#139876,#139877,#139878,#139879,#139880,#139881,#139882,
#139883,#139884,#139885,#139886,#139887,#139888,#139889,#139890,#139891,
#139892,#139893,#139894,#139895,#139896,#139897,#139898,#139899,#139900,
#139901,#139902,#139903,#139904,#139905,#139906,#139907,#139908,#139909,
#139910,#139911,#139912,#139913,#139914,#139915,#139916,#139917,#139918,
#139919,#139920),.UNSPECIFIED.,.F.,.F.,(4,3,3,3,3,3,3,3,3,3,3,3,3,3,3,3,
3,3,3,3,3,3,3,3,3,3,3,3,3,3,3,3,3,3,3,3,3,3,3,3,3,4),(78.539816339745,78.6377138097037,
78.7346673304385,78.831578691398,78.9284788661294,79.0271081744506,79.1241353185128,
79.2235657089636,79.3229960994143,79.421594224418,79.5200520071949,79.6202745749676,
79.7185541326958,79.8168007117691,79.9150437948075,80.0167409834497,80.1151253968685,
80.2184789731224,80.3218325493762,80.4204306743799,80.5188884571567,80.6191110249294,
80.7173905826575,80.8156371617308,80.9138802447693,81.0155774334115,81.1139618468302,
81.2173154230841,81.320668999338,81.4192671243417,81.5177249071184,81.6179474748911,
81.7162270326192,81.8144736116927,81.912716694731,82.0144138833732,82.112798296792,
82.2161518730459,82.3195054492999,82.4180964129928,82.516536214131,82.5977152967569),
 .UNSPECIFIED.);
#1413=B_SPLINE_CURVE_WITH_KNOTS('',3,(#139926,#139927,#139928,#139929,#139930,
#139931,#139932,#139933),.UNSPECIFIED.,.F.,.F.,(4,1,1,1,1,4),(84.8230070319889,
85.7808215317051,86.779657981667,87.7784944316289,88.7773308815907,88.8809435767746),
 .UNSPECIFIED.);
#1414=B_SPLINE_CURVE_WITH_KNOTS('',3,(#139934,#139935,#139936,#139937,#139938,
#139939,#139940,#139941,#139942,#139943,#139944,#139945,#139946,#139947,
#139948,#139949,#139950,#139951,#139952,#139953,#139954,#139955,#139956,
#139957,#139958,#139959,#139960,#139961,#139962,#139963,#139964,#139965,
#139966,#139967,#139968,#139969,#139970,#139971,#139972,#139973,#139974,
#139975,#139976,#139977,#139978,#139979,#139980,#139981,#139982,#139983,
#139984,#139985,#139986,#139987,#139988,#139989,#139990,#139991,#139992,
#139993,#139994,#139995,#139996,#139997,#139998,#139999,#140000,#140001,
#140002,#140003),.UNSPECIFIED.,.F.,.F.,(4,3,3,3,3,3,3,3,3,3,3,3,3,3,3,3,
3,3,3,3,3,3,3,4),(82.5965697553975,82.6951414213286,82.7843121818195,82.8829103068232,
82.9813680896,83.0815906573726,83.1798702151008,83.2781167941742,83.3763598772127,
83.4780570658549,83.5764414792737,83.6797950555275,83.7831486317814,83.8817467567851,
83.9802045395617,84.0804271073344,84.1787066650626,84.276953244136,84.3751963271744,
84.4768935158166,84.5752779292354,84.6786315054893,84.7819850817432,84.8230016469246),
 .UNSPECIFIED.);
#1415=B_SPLINE_CURVE_WITH_KNOTS('',3,(#140005,#140006,#140007,#140008,#140009,
#140010,#140011,#140012,#140013,#140014,#140015,#140016,#140017,#140018,
#140019,#140020,#140021,#140022,#140023,#140024,#140025,#140026,#140027,
#140028,#140029,#140030,#140031,#140032,#140033,#140034,#140035,#140036,
#140037,#140038,#140039,#140040,#140041,#140042,#140043,#140044,#140045,
#140046,#140047,#140048,#140049,#140050,#140051,#140052,#140053,#140054,
#140055,#140056,#140057,#140058,#140059,#140060,#140061,#140062,#140063,
#140064,#140065,#140066,#140067,#140068,#140069,#140070,#140071,#140072,
#140073,#140074),.UNSPECIFIED.,.F.,.F.,(4,3,3,3,3,3,3,3,3,3,3,3,3,3,3,3,
3,3,3,3,3,3,3,4),(82.5977152967569,82.6960046676817,82.794255337806,82.892496795247,
82.9907585104692,83.0891304667538,83.1875671193328,83.2861621863113,83.3183418992618,
83.4169400242654,83.5153978070423,83.615620374815,83.713899932543,83.8121465116164,
83.9103895946548,84.0120867832971,84.1104711967159,84.2138247729698,84.3171783492237,
84.420557830251,84.523654386749,84.6265834813182,84.7292989065994,84.8230016469246),
 .UNSPECIFIED.);
#1416=B_SPLINE_CURVE_WITH_KNOTS('',3,(#140075,#140076,#140077,#140078,#140079,
#140080,#140081,#140082,#140083,#140084,#140085,#140086,#140087,#140088,
#140089,#140090,#140091,#140092,#140093,#140094,#140095,#140096,#140097,
#140098,#140099,#140100,#140101,#140102,#140103,#140104,#140105,#140106,
#140107,#140108,#140109,#140110,#140111,#140112,#140113,#140114,#140115,
#140116,#140117,#140118,#140119,#140120,#140121,#140122,#140123,#140124,
#140125,#140126,#140127,#140128,#140129,#140130,#140131,#140132,#140133,
#140134,#140135,#140136,#140137,#140138,#140139,#140140,#140141,#140142,
#140143,#140144,#140145,#140146,#140147,#140148,#140149,#140150,#140151,
#140152,#140153,#140154,#140155,#140156,#140157,#140158,#140159,#140160,
#140161,#140162,#140163,#140164,#140165,#140166,#140167,#140168,#140169,
#140170,#140171,#140172,#140173,#140174,#140175,#140176,#140177,#140178,
#140179,#140180,#140181,#140182,#140183,#140184,#140185,#140186,#140187,
#140188,#140189,#140190,#140191,#140192,#140193,#140194,#140195,#140196,
#140197,#140198),.UNSPECIFIED.,.F.,.F.,(4,3,3,3,3,3,3,3,3,3,3,3,3,3,3,3,
3,3,3,3,3,3,3,3,3,3,3,3,3,3,3,3,3,3,3,3,3,3,3,3,3,4),(84.8230016472006,
84.9261861619503,85.029664796698,85.133294590709,85.2372126194223,85.3160147991855,
85.4146129241892,85.513070706966,85.6132932747387,85.7115728324668,85.8098194115402,
85.9080624945788,86.0097596832209,86.1081440966397,86.2114976728936,86.3148512491474,
86.4134493741511,86.5119071569278,86.6121297247005,86.7104092824287,86.8086558615021,
86.9068989445406,87.0085961331828,87.1069805466016,87.2103341228554,87.3136876991093,
87.412285824113,87.5107436068897,87.6109661746624,87.7092457323905,87.8074923114639,
87.9057353945024,88.0074325831446,88.1058169965634,88.2091705728173,88.3125241490712,
88.4111137865008,88.5095698168543,88.6079122101835,88.7061871882851,88.8044419893987,
88.8801389722626),.UNSPECIFIED.);
#1417=B_SPLINE_CURVE_WITH_KNOTS('',3,(#140204,#140205,#140206,#140207,#140208,
#140209,#140210,#140211,#140212,#140213,#140214,#140215,#140216,#140217,
#140218,#140219,#140220,#140221,#140222,#140223,#140224,#140225,#140226,
#140227,#140228,#140229,#140230,#140231,#140232,#140233,#140234,#140235,
#140236,#140237,#140238,#140239,#140240,#140241,#140242,#140243,#140244,
#140245,#140246,#140247,#140248,#140249,#140250,#140251,#140252,#140253,
#140254,#140255,#140256,#140257,#140258,#140259,#140260,#140261,#140262,
#140263,#140264,#140265,#140266,#140267,#140268,#140269,#140270,#140271,
#140272,#140273,#140274,#140275,#140276,#140277,#140278,#140279,#140280,
#140281,#140282,#140283,#140284,#140285,#140286,#140287,#140288,#140289,
#140290,#140291,#140292,#140293,#140294,#140295,#140296,#140297,#140298,
#140299,#140300,#140301,#140302,#140303,#140304,#140305,#140306,#140307,
#140308,#140309,#140310,#140311,#140312,#140313,#140314,#140315,#140316,
#140317,#140318,#140319,#140320,#140321,#140322,#140323,#140324,#140325,
#140326,#140327),.UNSPECIFIED.,.F.,.F.,(4,3,3,3,3,3,3,3,3,3,3,3,3,3,3,3,
3,3,3,3,3,3,3,3,3,3,3,3,3,3,3,3,3,3,3,3,3,3,3,3,3,4),(91.1061869541041,
91.2043419644769,91.3024795334306,91.4006291648835,91.4988897541851,91.5972075103073,
91.6957053368608,91.7738402314764,91.8724383564801,91.9708961392569,92.0711187070296,
92.1693982647577,92.2676448438311,92.3658879268697,92.4675851155118,92.5659695289307,
92.6693231051844,92.7726766814382,92.8712748064418,92.9697325892187,93.0699551569914,
93.1682347147194,93.2664812937929,93.3647243768315,93.4664215654736,93.5648059788925,
93.6681595551463,93.7715131314001,93.8701112564039,93.9685690391807,94.0687916069534,
94.1670711646815,94.2653177437549,94.3635608267936,94.4652580154357,94.5636424288545,
94.6669960051082,94.770349581362,94.8689185475017,94.9673651079953,95.0657083030438,
95.1638473593045),.UNSPECIFIED.);
#1418=B_SPLINE_CURVE_WITH_KNOTS('',3,(#140328,#140329,#140330,#140331,#140332,
#140333),.UNSPECIFIED.,.F.,.F.,(4,1,1,4),(88.8809435767746,89.7761673315526,
90.7750037815145,91.1061798190739),.UNSPECIFIED.);
#1419=B_SPLINE_CURVE_WITH_KNOTS('',3,(#140335,#140336,#140337,#140338,#140339,
#140340,#140341,#140342,#140343,#140344,#140345,#140346,#140347,#140348,
#140349,#140350,#140351,#140352,#140353,#140354,#140355,#140356,#140357,
#140358,#140359,#140360,#140361,#140362,#140363,#140364,#140365,#140366,
#140367,#140368,#140369,#140370,#140371,#140372,#140373,#140374,#140375,
#140376,#140377,#140378,#140379,#140380,#140381,#140382,#140383,#140384,
#140385,#140386,#140387,#140388,#140389,#140390,#140391,#140392,#140393,
#140394,#140395,#140396,#140397,#140398,#140399,#140400,#140401,#140402,
#140403,#140404,#140405,#140406,#140407),.UNSPECIFIED.,.F.,.F.,(4,3,3,3,
3,3,3,3,3,3,3,3,3,3,3,3,3,3,3,3,3,3,3,3,4),(88.8801389722626,88.9783988165887,
89.0767679991754,89.1752004281995,89.2737928157651,89.311360599033,89.4099587240367,
89.5084165068134,89.6086390745861,89.7069186323143,89.8051652113877,89.9034082944262,
90.0051054830683,90.1034898964872,90.206843472741,90.3101970489949,90.409695787095,
90.5067185530535,90.6036495481492,90.70051989818,90.801936662084,90.8988156754798,
90.9957205549588,91.0927209416413,91.1061869537961),.UNSPECIFIED.);
#1420=B_SPLINE_CURVE_WITH_KNOTS('',3,(#140408,#140409,#140410,#140411,#140412,
#140413,#140414,#140415,#140416,#140417,#140418,#140419,#140420,#140421,
#140422,#140423,#140424,#140425,#140426,#140427,#140428,#140429,#140430,
#140431,#140432,#140433,#140434,#140435,#140436,#140437,#140438,#140439,
#140440,#140441,#140442,#140443,#140444,#140445,#140446,#140447,#140448,
#140449,#140450,#140451,#140452,#140453,#140454,#140455,#140456,#140457,
#140458,#140459,#140460,#140461,#140462,#140463,#140464,#140465,#140466,
#140467,#140468,#140469,#140470,#140471,#140472,#140473,#140474,#140475,
#140476,#140477,#140478,#140479,#140480,#140481,#140482,#140483,#140484,
#140485,#140486,#140487,#140488,#140489,#140490,#140491,#140492,#140493,
#140494,#140495,#140496,#140497,#140498,#140499,#140500,#140501,#140502,
#140503,#140504,#140505,#140506,#140507,#140508,#140509,#140510,#140511,
#140512,#140513,#140514,#140515,#140516,#140517,#140518,#140519,#140520,
#140521,#140522,#140523,#140524,#140525,#140526,#140527,#140528,#140529,
#140530,#140531),.UNSPECIFIED.,.F.,.F.,(4,3,3,3,3,3,3,3,3,3,3,3,3,3,3,3,
3,3,3,3,3,3,3,3,3,3,3,3,3,3,3,3,3,3,3,3,3,3,3,3,3,4),(91.1061869541041,
91.2465035596788,91.3090334989568,91.4076316239605,91.5060894067373,91.6063119745099,
91.7045915322381,91.8028381113114,91.90108119435,92.0027783829921,92.1011627964109,
92.2045163726648,92.3078699489186,92.4064680739223,92.5049258566991,92.6051484244718,
92.7034279821999,92.8016745612733,92.8999176443119,93.001614832954,93.0999992463728,
93.2033528226267,93.3067063988805,93.4053045238842,93.5037623066609,93.6039848744336,
93.7022644321617,93.8005110112351,93.8987540942736,94.0004512829158,94.0988356963346,
94.2021892725885,94.3055428488424,94.4041508037225,94.502589190302,94.6009312472693,
94.6992065724876,94.7974446925382,94.8957159603398,94.9940021460021,95.0923959722183,
95.1629909762769),.UNSPECIFIED.);
#1421=B_SPLINE_CURVE_WITH_KNOTS('',3,(#140537,#140538,#140539,#140540,#140541,
#140542,#140543,#140544),.UNSPECIFIED.,.F.,.F.,(4,1,1,1,1,4),(97.389379769506,
97.7668589312476,98.7656953812095,99.7645318311714,100.763368281133,101.445902010813),
 .UNSPECIFIED.);
#1422=B_SPLINE_CURVE_WITH_KNOTS('',3,(#140545,#140546,#140547,#140548,#140549,
#140550,#140551,#140552,#140553,#140554,#140555,#140556,#140557,#140558,
#140559,#140560,#140561,#140562,#140563,#140564,#140565,#140566,#140567,
#140568,#140569,#140570,#140571,#140572,#140573,#140574,#140575,#140576,
#140577,#140578,#140579,#140580,#140581,#140582,#140583,#140584,#140585,
#140586,#140587,#140588,#140589,#140590,#140591,#140592,#140593,#140594,
#140595,#140596,#140597,#140598,#140599,#140600,#140601,#140602,#140603,
#140604,#140605,#140606,#140607,#140608,#140609,#140610,#140611,#140612,
#140613,#140614,#140615,#140616,#140617),.UNSPECIFIED.,.F.,.F.,(4,3,3,3,
3,3,3,3,3,3,3,3,3,3,3,3,3,3,3,3,3,3,3,3,4),(95.1638473593045,95.2620943271636,
95.3603371810261,95.4625493936005,95.5609329069904,95.6593867641743,95.7579931965668,
95.7691860313239,95.8677841563275,95.9662419391043,96.066464506877,96.1647440646051,
96.2629906436785,96.361233726717,96.4629309153592,96.5613153287779,96.6646689050318,
96.7680224812857,96.867499372579,96.9668292609829,97.0660403563902,97.1651524247998,
97.264207533224,97.3632407686273,97.3893722612837),.UNSPECIFIED.);
#1423=B_SPLINE_CURVE_WITH_KNOTS('',3,(#140619,#140620,#140621,#140622,#140623,
#140624,#140625,#140626,#140627,#140628,#140629,#140630,#140631,#140632,
#140633,#140634,#140635,#140636,#140637,#140638,#140639,#140640,#140641,
#140642,#140643,#140644,#140645,#140646,#140647,#140648,#140649,#140650,
#140651,#140652,#140653,#140654,#140655,#140656,#140657,#140658,#140659,
#140660,#140661,#140662,#140663,#140664,#140665,#140666,#140667,#140668,
#140669,#140670,#140671,#140672,#140673,#140674,#140675,#140676,#140677,
#140678,#140679,#140680,#140681,#140682,#140683,#140684,#140685,#140686,
#140687,#140688),.UNSPECIFIED.,.F.,.F.,(4,3,3,3,3,3,3,3,3,3,3,3,3,3,3,3,
3,3,3,3,3,3,3,4),(95.1629909762769,95.2615808559533,95.3043792988043,95.402977423808,
95.5014352065847,95.6016577743574,95.6999373320855,95.7981839111589,95.8964269941974,
95.9981241828396,96.0965085962583,96.1998621725122,96.3032157487661,96.4018138737698,
96.5002716565465,96.6004942243192,96.6987737820473,96.7970203611207,96.8952634441592,
96.9969606328014,97.0953450462202,97.1986986224741,97.302052198728,97.3893722612837),
 .UNSPECIFIED.);
#1424=B_SPLINE_CURVE_WITH_KNOTS('',3,(#140689,#140690,#140691,#140692,#140693,
#140694,#140695,#140696),.UNSPECIFIED.,.F.,.F.,(4,1,1,1,1,4),(97.3893809713061,
98.3008886486899,99.2997250986518,100.298561548614,101.297397998576,101.447496672416),
 .UNSPECIFIED.);
#1425=B_SPLINE_CURVE_WITH_KNOTS('',3,(#140702,#140703,#140704,#140705,#140706,
#140707,#140708,#140709,#140710,#140711,#140712,#140713,#140714,#140715,
#140716,#140717,#140718,#140719,#140720,#140721,#140722,#140723,#140724,
#140725,#140726,#140727,#140728,#140729,#140730,#140731,#140732,#140733,
#140734,#140735,#140736,#140737,#140738,#140739,#140740,#140741,#140742,
#140743,#140744,#140745,#140746,#140747,#140748,#140749,#140750,#140751,
#140752,#140753,#140754,#140755,#140756,#140757,#140758,#140759,#140760,
#140761,#140762,#140763,#140764,#140765,#140766,#140767,#140768,#140769,
#140770,#140771,#140772,#140773,#140774,#140775,#140776,#140777,#140778,
#140779,#140780,#140781,#140782,#140783,#140784,#140785,#140786,#140787,
#140788,#140789,#140790,#140791,#140792,#140793,#140794,#140795,#140796,
#140797,#140798,#140799,#140800,#140801,#140802,#140803,#140804,#140805,
#140806,#140807,#140808,#140809,#140810,#140811,#140812,#140813,#140814,
#140815,#140816,#140817,#140818,#140819,#140820,#140821,#140822,#140823,
#140824,#140825),.UNSPECIFIED.,.F.,.F.,(4,3,3,3,3,3,3,3,3,3,3,3,3,3,3,3,
3,3,3,3,3,3,3,3,3,3,3,3,3,3,3,3,3,3,3,3,3,3,3,3,3,4),(103.672557568463,
103.759877631019,103.858475756023,103.9569335388,104.057156106572,104.1554356643,
104.253682243374,104.351925326412,104.453622515055,104.552006928473,104.655360504727,
104.758714080981,104.857312205985,104.955769988761,105.055992556534,105.154272114262,
105.252518693336,105.350761776374,105.452458965016,105.550843378435,105.654196954689,
105.757550530943,105.856148655947,105.954606438723,106.054829006496,106.153108564224,
106.251355143297,106.349598226336,106.451295414978,106.549679828396,106.65303340465,
106.756386980904,106.854986798946,106.953445809625,107.051788768338,107.150068003062,
107.248313037023,107.346553353057,107.444881222511,107.543251670472,107.641785788201,
107.729756577966),.UNSPECIFIED.);
#1426=B_SPLINE_CURVE_WITH_KNOTS('',3,(#140826,#140827,#140828,#140829,#140830,
#140831),.UNSPECIFIED.,.F.,.F.,(4,1,1,4),(101.445902010813,101.762204731095,
102.761041181057,103.672548858934),.UNSPECIFIED.);
#1427=B_SPLINE_CURVE_WITH_KNOTS('',3,(#140833,#140834,#140835,#140836,#140837,
#140838),.UNSPECIFIED.,.F.,.F.,(4,1,1,4),(101.447496672416,102.296234448537,
103.295070898499,103.672550060693),.UNSPECIFIED.);
#1428=B_SPLINE_CURVE_WITH_KNOTS('',3,(#140839,#140840,#140841,#140842,#140843,
#140844,#140845,#140846,#140847,#140848,#140849,#140850,#140851,#140852,
#140853,#140854,#140855,#140856,#140857,#140858,#140859,#140860,#140861,
#140862,#140863,#140864,#140865,#140866,#140867,#140868,#140869,#140870,
#140871,#140872,#140873,#140874,#140875,#140876,#140877,#140878,#140879,
#140880,#140881,#140882,#140883,#140884,#140885,#140886,#140887,#140888,
#140889,#140890,#140891,#140892,#140893,#140894,#140895,#140896,#140897,
#140898,#140899,#140900,#140901,#140902,#140903,#140904,#140905,#140906,
#140907,#140908,#140909,#140910,#140911,#140912,#140913,#140914,#140915,
#140916,#140917,#140918,#140919,#140920,#140921,#140922,#140923,#140924,
#140925,#140926,#140927,#140928,#140929,#140930,#140931,#140932,#140933,
#140934,#140935,#140936,#140937,#140938,#140939,#140940,#140941,#140942,
#140943,#140944,#140945,#140946,#140947,#140948,#140949,#140950,#140951,
#140952,#140953,#140954,#140955,#140956,#140957,#140958,#140959,#140960,
#140961,#140962,#140963,#140964,#140965),.UNSPECIFIED.,.F.,.F.,(4,3,3,3,
3,3,3,3,3,3,3,3,3,3,3,3,3,3,3,3,3,3,3,3,3,3,3,3,3,3,3,3,3,3,3,3,3,3,3,3,
3,3,4),(103.672557568463,103.771601702603,103.870660322484,103.96976131202,
104.06899945985,104.168318657834,104.267812431338,104.293907348461,104.392505473465,
104.490963256242,104.591185824014,104.689465381742,104.787711960816,104.885955043854,
104.987652232496,105.086036645915,105.189390222169,105.292743798423,105.391341923427,
105.489799706204,105.590022273976,105.688301831704,105.786548410778,105.884791493816,
105.986488682458,106.084873095877,106.188226672131,106.291580248385,106.390178373389,
106.488636156165,106.588858723938,106.687138281666,106.78538486074,106.883627943778,
106.98532513242,107.083709545839,107.187063122093,107.290416698347,107.389023062568,
107.487464394916,107.585810440419,107.68408611143,107.730086449126),
 .UNSPECIFIED.);
#1429=B_SPLINE_CURVE_WITH_KNOTS('',3,(#140971,#140972,#140973,#140974,#140975,
#140976,#140977,#140978,#140979,#140980,#140981,#140982,#140983,#140984,
#140985,#140986,#140987,#140988,#140989,#140990,#140991,#140992,#140993,
#140994,#140995,#140996,#140997,#140998,#140999,#141000,#141001,#141002,
#141003,#141004,#141005,#141006,#141007,#141008,#141009,#141010,#141011,
#141012,#141013,#141014,#141015,#141016,#141017,#141018,#141019,#141020,
#141021,#141022,#141023,#141024,#141025,#141026,#141027,#141028,#141029,
#141030,#141031,#141032,#141033,#141034,#141035,#141036,#141037,#141038,
#141039,#141040,#141041,#141042,#141043,#141044,#141045,#141046,#141047,
#141048,#141049,#141050,#141051,#141052,#141053,#141054,#141055,#141056,
#141057,#141058,#141059,#141060,#141061,#141062,#141063,#141064,#141065,
#141066,#141067,#141068,#141069,#141070,#141071,#141072,#141073,#141074,
#141075,#141076,#141077,#141078,#141079,#141080,#141081,#141082,#141083,
#141084,#141085,#141086,#141087,#141088,#141089,#141090,#141091,#141092,
#141093,#141094,#141095,#141096,#141097),.UNSPECIFIED.,.F.,.F.,(4,3,3,3,
3,3,3,3,3,3,3,3,3,3,3,3,3,3,3,3,3,3,3,3,3,3,3,3,3,3,3,3,3,3,3,3,3,3,3,3,
3,3,4),(109.955742875951,110.055241614051,110.152151423466,110.249014842069,
110.345862894414,110.447330365999,110.544300028994,110.641334438529,110.738518045248,
110.751732780752,110.850330905756,110.948788688532,111.049011256305,111.147290814033,
111.245537393107,111.343780476145,111.445477664787,111.543862078206,111.64721565446,
111.750569230714,111.849167355718,111.947625138495,112.047847706267,112.146127263996,
112.244373843069,112.342616926107,112.44431411475,112.542698528168,112.646052104422,
112.749405680676,112.84800380568,112.946461588456,113.046684156229,113.144963713957,
113.24321029303,113.341453376069,113.443150564711,113.54153497813,113.644888554384,
113.748242130638,113.846836224879,113.945278284695,114.013656833936),
 .UNSPECIFIED.);
#1430=B_SPLINE_CURVE_WITH_KNOTS('',3,(#141098,#141099,#141100,#141101,#141102,
#141103,#141104,#141105,#141106,#141107,#141108,#141109,#141110,#141111,
#141112,#141113,#141114,#141115,#141116,#141117,#141118,#141119,#141120,
#141121,#141122,#141123,#141124,#141125,#141126,#141127,#141128,#141129,
#141130,#141131,#141132,#141133,#141134,#141135,#141136,#141137,#141138,
#141139,#141140,#141141,#141142,#141143,#141144,#141145,#141146,#141147,
#141148,#141149,#141150,#141151,#141152,#141153,#141154,#141155,#141156,
#141157,#141158,#141159,#141160,#141161,#141162,#141163,#141164,#141165,
#141166,#141167),.UNSPECIFIED.,.F.,.F.,(4,3,3,3,3,3,3,3,3,3,3,3,3,3,3,3,
3,3,3,3,3,3,3,4),(107.729756577966,107.755223430866,107.85382155587,107.952279338647,
108.052501906419,108.150781464147,108.249028043221,108.347271126259,108.448968314901,
108.54735272832,108.650706304574,108.754059880828,108.852658005832,108.951115788608,
109.051338356381,109.149617914109,109.247864493183,109.346107576221,109.447804764863,
109.546189178282,109.649542754536,109.75289633079,109.893212936358,109.955742875643),
 .UNSPECIFIED.);
#1431=B_SPLINE_CURVE_WITH_KNOTS('',3,(#141169,#141170,#141171,#141172,#141173,
#141174,#141175,#141176,#141177,#141178,#141179,#141180,#141181,#141182,
#141183,#141184,#141185,#141186,#141187,#141188,#141189,#141190,#141191,
#141192,#141193,#141194,#141195,#141196,#141197,#141198,#141199,#141200,
#141201,#141202,#141203,#141204,#141205,#141206,#141207,#141208,#141209,
#141210,#141211,#141212,#141213,#141214,#141215,#141216,#141217,#141218,
#141219,#141220,#141221,#141222,#141223,#141224,#141225,#141226,#141227,
#141228,#141229,#141230,#141231,#141232,#141233,#141234,#141235,#141236,
#141237,#141238),.UNSPECIFIED.,.F.,.F.,(4,3,3,3,3,3,3,3,3,3,3,3,3,3,3,3,
3,3,3,3,3,3,3,4),(107.730086449126,107.828327813024,107.926578911936,108.024934198482,
108.123344723364,108.221924067715,108.289253148309,108.387851273313,108.48630905609,
108.586531623862,108.684811181591,108.783057760664,108.881300843703,108.982998032345,
109.081382445763,109.184736022017,109.288089598271,109.386591328535,109.484956309733,
109.583214317042,109.681399820024,109.779540599734,109.877698313765,109.955742875643),
 .UNSPECIFIED.);
#1432=B_SPLINE_CURVE_WITH_KNOTS('',3,(#141239,#141240,#141241,#141242,#141243,
#141244,#141245,#141246),.UNSPECIFIED.,.F.,.F.,(4,1,1,1,1,4),(109.955750010087,
110.286926048232,111.285762498194,112.284598948156,113.283435398118,114.012186970914),
 .UNSPECIFIED.);
#1433=B_SPLINE_CURVE_WITH_KNOTS('',3,(#141252,#141253,#141254,#141255,#141256,
#141257,#141258,#141259,#141260,#141261,#141262,#141263,#141264,#141265,
#141266,#141267,#141268,#141269,#141270,#141271,#141272,#141273,#141274,
#141275,#141276,#141277,#141278,#141279,#141280,#141281,#141282,#141283,
#141284,#141285,#141286,#141287,#141288,#141289,#141290,#141291,#141292,
#141293,#141294,#141295,#141296,#141297,#141298,#141299,#141300,#141301,
#141302,#141303,#141304,#141305,#141306,#141307,#141308,#141309,#141310,
#141311,#141312,#141313,#141314,#141315,#141316,#141317,#141318,#141319,
#141320,#141321,#141322,#141323,#141324,#141325,#141326,#141327,#141328,
#141329,#141330,#141331,#141332,#141333,#141334,#141335,#141336,#141337,
#141338,#141339,#141340,#141341,#141342,#141343,#141344,#141345,#141346,
#141347,#141348,#141349,#141350,#141351,#141352,#141353,#141354,#141355,
#141356,#141357,#141358,#141359,#141360,#141361,#141362,#141363,#141364,
#141365,#141366,#141367,#141368,#141369,#141370,#141371,#141372,#141373,
#141374,#141375),.UNSPECIFIED.,.F.,.F.,(4,3,3,3,3,3,3,3,3,3,3,3,3,3,3,3,
3,3,3,3,3,3,3,3,3,3,3,3,3,3,3,3,3,3,3,3,3,3,3,3,3,4),(116.238928182823,
116.341566510357,116.44447107289,116.547509821617,116.650828963887,116.744751480523,
116.843349605527,116.941807388303,117.042029956076,117.140309513804,117.238556092878,
117.336799175916,117.438496364558,117.536880777977,117.640234354231,117.743587930485,
117.842186055489,117.940643838266,118.040866406038,118.139145963766,118.23739254284,
118.335635625878,118.437332814521,118.535717227939,118.639070804193,118.742424380447,
118.841022505451,118.939480288228,119.039702856,119.137982413728,119.236228992802,
119.33447207584,119.436169264482,119.534553677901,119.637907254155,119.741260830409,
119.839851983055,119.9383091947,120.03665133111,120.134925920017,120.2331760742,
120.296103423185),.UNSPECIFIED.);
#1434=B_SPLINE_CURVE_WITH_KNOTS('',3,(#141376,#141377,#141378,#141379,#141380,
#141381,#141382,#141383,#141384,#141385,#141386,#141387,#141388,#141389,
#141390,#141391,#141392,#141393,#141394,#141395,#141396,#141397,#141398,
#141399,#141400,#141401,#141402,#141403,#141404,#141405,#141406,#141407,
#141408,#141409,#141410,#141411,#141412,#141413,#141414,#141415,#141416,
#141417,#141418,#141419,#141420,#141421,#141422,#141423,#141424,#141425,
#141426,#141427,#141428,#141429,#141430,#141431,#141432,#141433,#141434,
#141435,#141436,#141437,#141438,#141439,#141440,#141441,#141442,#141443,
#141444,#141445),.UNSPECIFIED.,.F.,.F.,(4,3,3,3,3,3,3,3,3,3,3,3,3,3,3,3,
3,3,3,3,3,3,3,4),(114.013656833936,114.111953411531,114.210207448244,114.308448436441,
114.406705847382,114.505071337775,114.603498076973,114.702086932435,114.747078580599,
114.845676705603,114.94413448838,115.044357056152,115.14263661388,115.240883192954,
115.339126275992,115.440823464634,115.539207878053,115.642561454307,115.745915030561,
115.84988875933,115.953561696348,116.057054365164,116.160309146371,116.238928182547),
 .UNSPECIFIED.);
#1435=B_SPLINE_CURVE_WITH_KNOTS('',3,(#141447,#141448,#141449,#141450,#141451,
#141452),.UNSPECIFIED.,.F.,.F.,(4,1,1,4),(114.012186970914,114.28227184808,
115.281108298042,116.2389227975),.UNSPECIFIED.);
#1436=B_SPLINE_CURVE_WITH_KNOTS('',3,(#141453,#141454,#141455,#141456,#141457,
#141458,#141459,#141460,#141461,#141462,#141463,#141464,#141465,#141466,
#141467,#141468,#141469,#141470,#141471,#141472,#141473,#141474,#141475,
#141476,#141477,#141478,#141479,#141480,#141481,#141482,#141483,#141484,
#141485,#141486,#141487,#141488,#141489,#141490,#141491,#141492,#141493,
#141494,#141495,#141496,#141497,#141498,#141499,#141500,#141501,#141502,
#141503,#141504,#141505,#141506,#141507,#141508,#141509,#141510,#141511,
#141512,#141513,#141514,#141515,#141516,#141517,#141518,#141519,#141520,
#141521,#141522,#141523,#141524,#141525,#141526,#141527,#141528,#141529,
#141530,#141531,#141532,#141533,#141534,#141535,#141536,#141537,#141538,
#141539,#141540,#141541,#141542,#141543,#141544,#141545,#141546,#141547,
#141548,#141549,#141550,#141551,#141552,#141553,#141554,#141555,#141556,
#141557,#141558,#141559,#141560,#141561,#141562,#141563,#141564,#141565,
#141566,#141567,#141568,#141569,#141570,#141571,#141572,#141573,#141574,
#141575,#141576,#141577,#141578,#141579),.UNSPECIFIED.,.F.,.F.,(4,3,3,3,
3,3,3,3,3,3,3,3,3,3,3,3,3,3,3,3,3,3,3,3,3,3,3,3,3,3,3,3,3,3,3,3,3,3,3,3,
3,3,4),(116.238928182823,116.279944748004,116.378542873008,116.477000655784,
116.577223223557,116.675502781285,116.773749360358,116.871992443397,116.973689632039,
117.072074045458,117.175427621712,117.278781197966,117.37737932297,117.475837105746,
117.576059673519,117.674339231247,117.77258581032,117.870828893359,117.972526082001,
118.07091049542,118.174264071673,118.277617647927,118.376215772931,118.474673555707,
118.57489612348,118.673175681208,118.771422260282,118.86966534332,118.971362531962,
119.069746945381,119.173100521635,119.276454097889,119.375052222893,119.47351000567,
119.573732573442,119.67201213117,119.770258710244,119.868501793282,119.970198981924,
120.068583395343,120.171936971597,120.275290547851,120.296396941981),
 .UNSPECIFIED.);
#1437=B_SPLINE_CURVE_WITH_KNOTS('',3,(#141585,#141586,#141587,#141588,#141589,
#141590,#141591,#141592),.UNSPECIFIED.,.F.,.F.,(4,1,1,1,1,4),(122.522113490002,
122.737770180294,123.736606630256,124.735443080218,125.73427953018,126.578666843287),
 .UNSPECIFIED.);
#1438=B_SPLINE_CURVE_WITH_KNOTS('',3,(#141593,#141594,#141595,#141596,#141597,
#141598,#141599,#141600,#141601,#141602,#141603,#141604,#141605,#141606,
#141607,#141608,#141609,#141610,#141611,#141612,#141613,#141614,#141615,
#141616,#141617,#141618,#141619,#141620,#141621,#141622,#141623,#141624,
#141625,#141626,#141627,#141628,#141629,#141630,#141631,#141632,#141633,
#141634,#141635,#141636,#141637,#141638,#141639,#141640,#141641,#141642,
#141643,#141644,#141645,#141646,#141647,#141648,#141649,#141650,#141651,
#141652,#141653,#141654,#141655,#141656,#141657,#141658,#141659,#141660,
#141661,#141662),.UNSPECIFIED.,.F.,.F.,(4,3,3,3,3,3,3,3,3,3,3,3,3,3,3,3,
3,3,3,3,3,3,3,4),(120.296103423185,120.394359176955,120.492722088099,120.591144801905,
120.689731215843,120.740097280371,120.838695405375,120.937153188151,121.037375755924,
121.135655313652,121.233901892726,121.332144975764,121.433842164406,121.532226577825,
121.635580154079,121.738933730333,121.836831200292,121.933909156543,122.030894120917,
122.127817176647,122.226391254986,122.323316910845,122.422715200423,122.522113490002),
 .UNSPECIFIED.);
#1439=B_SPLINE_CURVE_WITH_KNOTS('',3,(#141664,#141665,#141666,#141667,#141668,
#141669,#141670,#141671,#141672,#141673,#141674,#141675,#141676,#141677,
#141678,#141679,#141680,#141681,#141682,#141683,#141684,#141685,#141686,
#141687,#141688,#141689,#141690,#141691,#141692,#141693,#141694,#141695,
#141696,#141697,#141698,#141699,#141700,#141701,#141702,#141703,#141704,
#141705,#141706,#141707,#141708,#141709,#141710,#141711,#141712,#141713,
#141714,#141715,#141716,#141717,#141718,#141719,#141720,#141721,#141722,
#141723,#141724,#141725,#141726,#141727,#141728,#141729,#141730),
 .UNSPECIFIED.,.F.,.F.,(4,3,3,3,3,3,3,3,3,3,3,3,3,3,3,3,3,3,3,3,3,3,4),
(120.296396941981,120.394962276094,120.493394302568,120.591721864652,120.689992682742,
120.788236268825,120.886482101004,120.984827578214,121.083221565444,121.18179225211,
121.274126997813,121.372725122817,121.471182905594,121.571405473366,121.669685031094,
121.767931610168,121.866174693206,121.967871881848,122.066256295267,122.169609871521,
122.272963447775,122.40085782982,122.522113389975),.UNSPECIFIED.);
#1440=B_SPLINE_CURVE_WITH_KNOTS('',3,(#141731,#141732,#141733,#141734,#141735,
#141736,#141737,#141738),.UNSPECIFIED.,.F.,.F.,(4,1,1,1,1,4),(122.522113490002,
123.271799897737,124.270636347699,125.26947279766,126.268309247622,126.580285776533),
 .UNSPECIFIED.);
#1441=B_SPLINE_CURVE_WITH_KNOTS('',3,(#141744,#141745,#141746,#141747,#141748,
#141749,#141750,#141751,#141752,#141753,#141754,#141755,#141756,#141757,
#141758,#141759,#141760,#141761,#141762,#141763,#141764,#141765,#141766,
#141767,#141768,#141769,#141770,#141771,#141772,#141773,#141774,#141775,
#141776,#141777,#141778,#141779,#141780,#141781,#141782,#141783,#141784,
#141785,#141786,#141787,#141788,#141789,#141790,#141791,#141792,#141793,
#141794,#141795,#141796,#141797,#141798,#141799,#141800,#141801,#141802,
#141803,#141804,#141805,#141806,#141807,#141808,#141809,#141810,#141811,
#141812,#141813,#141814,#141815,#141816,#141817,#141818,#141819,#141820,
#141821,#141822,#141823,#141824,#141825,#141826,#141827,#141828,#141829,
#141830,#141831,#141832,#141833,#141834,#141835,#141836,#141837,#141838,
#141839,#141840,#141841,#141842,#141843,#141844,#141845,#141846,#141847,
#141848,#141849,#141850,#141851,#141852,#141853,#141854,#141855,#141856,
#141857,#141858,#141859,#141860,#141861,#141862,#141863,#141864,#141865,
#141866,#141867,#141868,#141869,#141870),.UNSPECIFIED.,.F.,.F.,(4,3,3,3,
3,3,3,3,3,3,3,3,3,3,3,3,3,3,3,3,3,3,3,3,3,3,3,3,3,3,3,3,3,3,3,3,3,3,3,3,
3,3,4),(128.805298797182,128.902840431273,129.000250613517,129.097560812666,
129.194818343698,129.292053887498,129.389298094495,129.486642967569,129.584044330746,
129.681605924981,129.729625330028,129.828223455032,129.926681237808,130.026903805581,
130.125183363309,130.223429942382,130.321673025421,130.423370214063,130.521754627481,
130.625108203735,130.728461779989,130.827059904993,130.925517687769,131.025740255542,
131.12401981327,131.222266392343,131.320509475382,131.422206664024,131.520591077443,
131.623944653697,131.727298229951,131.825896354955,131.924354137732,132.024576705504,
132.122856263232,132.221102842306,132.319345925344,132.421043113986,132.519427527405,
132.622781103659,132.726134679913,132.824726637196,132.863178396459),
 .UNSPECIFIED.);
#1442=B_SPLINE_CURVE_WITH_KNOTS('',3,(#141871,#141872,#141873,#141874,#141875,
#141876,#141877),.UNSPECIFIED.,.F.,.F.,(4,1,1,1,4),(126.578666843287,126.733115980142,
127.731952430104,128.730788880066,128.805298797182),.UNSPECIFIED.);
#1443=B_SPLINE_CURVE_WITH_KNOTS('',3,(#141879,#141880,#141881,#141882,#141883,
#141884),.UNSPECIFIED.,.F.,.F.,(4,1,1,4),(126.580285776533,127.267145697584,
128.265982147546,128.805298797182),.UNSPECIFIED.);
#1444=B_SPLINE_CURVE_WITH_KNOTS('',3,(#141885,#141886,#141887,#141888,#141889,
#141890,#141891,#141892,#141893,#141894,#141895,#141896,#141897,#141898,
#141899,#141900,#141901,#141902,#141903,#141904,#141905,#141906,#141907,
#141908,#141909,#141910,#141911,#141912,#141913,#141914,#141915,#141916,
#141917,#141918,#141919,#141920,#141921,#141922,#141923,#141924,#141925,
#141926,#141927,#141928,#141929,#141930,#141931,#141932,#141933,#141934,
#141935,#141936,#141937,#141938,#141939,#141940,#141941,#141942,#141943,
#141944,#141945,#141946,#141947,#141948,#141949,#141950,#141951,#141952,
#141953,#141954,#141955,#141956,#141957,#141958,#141959,#141960,#141961,
#141962,#141963,#141964,#141965,#141966,#141967,#141968,#141969,#141970,
#141971,#141972,#141973,#141974,#141975,#141976,#141977,#141978,#141979,
#141980,#141981,#141982,#141983,#141984,#141985,#141986,#141987,#141988,
#141989,#141990,#141991,#141992,#141993,#141994,#141995,#141996,#141997,
#141998,#141999,#142000,#142001,#142002,#142003,#142004,#142005,#142006,
#142007,#142008),.UNSPECIFIED.,.F.,.F.,(4,3,3,3,3,3,3,3,3,3,3,3,3,3,3,3,
3,3,3,3,3,3,3,3,3,3,3,3,3,3,3,3,3,3,3,3,3,3,3,3,3,4),(128.805299011159,
128.91008561987,129.01525575915,129.120630109632,129.226318351047,129.264818597508,
129.363416722512,129.461874505288,129.562097073061,129.660376630789,129.758623209863,
129.856866292901,129.958563481543,130.056947894962,130.160301471216,130.26365504747,
130.362253172474,130.460710955251,130.560933523023,130.659213080751,130.757459659825,
130.855702742863,130.957399931506,131.055784344924,131.159137921178,131.262491497432,
131.361089622436,131.459547405212,131.559769972985,131.658049530713,131.756296109787,
131.854539192825,131.956236381467,132.054620794886,132.15797437114,132.261327947394,
132.359913784698,132.458366887932,132.559360493572,132.657635696798,132.759988503645,
132.862341310493),.UNSPECIFIED.);
#1445=B_SPLINE_CURVE_WITH_KNOTS('',3,(#142014,#142015,#142016,#142017,#142018,
#142019,#142020,#142021,#142022,#142023,#142024,#142025,#142026,#142027,
#142028,#142029,#142030,#142031,#142032,#142033,#142034,#142035,#142036,
#142037,#142038,#142039,#142040,#142041,#142042,#142043,#142044,#142045,
#142046,#142047,#142048,#142049,#142050,#142051,#142052,#142053,#142054,
#142055,#142056,#142057,#142058,#142059,#142060,#142061,#142062,#142063,
#142064,#142065,#142066,#142067,#142068,#142069,#142070,#142071,#142072,
#142073,#142074,#142075,#142076,#142077,#142078,#142079,#142080,#142081,
#142082,#142083,#142084,#142085,#142086,#142087,#142088,#142089,#142090,
#142091,#142092,#142093,#142094,#142095,#142096,#142097,#142098,#142099,
#142100,#142101,#142102,#142103,#142104,#142105,#142106,#142107,#142108,
#142109,#142110,#142111,#142112,#142113,#142114,#142115,#142116,#142117,
#142118,#142119,#142120,#142121,#142122,#142123,#142124,#142125,#142126,
#142127,#142128,#142129,#142130,#142131,#142132,#142133,#142134,#142135,
#142136,#142137,#142138,#142139,#142140),.UNSPECIFIED.,.F.,.F.,(4,3,3,3,
3,3,3,3,3,3,3,3,3,3,3,3,3,3,3,3,3,3,3,3,3,3,3,3,3,3,3,3,3,3,3,3,3,3,3,3,
3,3,4),(135.088484104361,135.187254556185,135.286029876604,135.384838499174,
135.483776463585,135.582788468008,135.681976179005,135.722644029799,135.821242154803,
135.919699937579,136.019922505352,136.11820206308,136.216448642154,136.314691725192,
136.416388913834,136.514773327253,136.618126903507,136.721480479761,136.820078604765,
136.918536387542,137.018758955314,137.117038513042,137.215285092116,137.313528175154,
137.415225363796,137.513609777215,137.616963353469,137.720316929723,137.818915054727,
137.917372837503,138.017595405276,138.115874963004,138.214121542077,138.312364625116,
138.414061813758,138.512446227176,138.61579980343,138.719153379684,138.817761602491,
138.916204188037,139.0145513523,139.112826031211,139.146050636314),
 .UNSPECIFIED.);
#1446=B_SPLINE_CURVE_WITH_KNOTS('',3,(#142141,#142142,#142143,#142144,#142145,
#142146,#142147,#142148,#142149,#142150,#142151,#142152,#142153,#142154,
#142155,#142156,#142157,#142158,#142159,#142160,#142161,#142162,#142163,
#142164,#142165,#142166,#142167,#142168,#142169,#142170,#142171,#142172,
#142173,#142174,#142175,#142176,#142177,#142178,#142179,#142180,#142181,
#142182,#142183,#142184,#142185,#142186,#142187,#142188,#142189,#142190,
#142191,#142192,#142193,#142194,#142195,#142196,#142197,#142198,#142199,
#142200,#142201,#142202,#142203,#142204,#142205,#142206,#142207,#142208,
#142209,#142210),.UNSPECIFIED.,.F.,.F.,(4,3,3,3,3,3,3,3,3,3,3,3,3,3,3,3,
3,3,3,3,3,3,3,4),(132.863178396459,132.961590313953,133.059905719281,133.15816959061,
133.256411432016,133.354660718376,133.453012823974,133.551418110189,133.649994583599,
133.724971129875,133.823569254879,133.922027037656,134.022249605428,134.120529163156,
134.21877574223,134.317018825268,134.41871601391,134.517100427329,134.620454003583,
134.723807579837,134.8363385207,134.948409000641,135.059693750754,135.088484104126),
 .UNSPECIFIED.);
#1447=B_SPLINE_CURVE_WITH_KNOTS('',3,(#142212,#142213,#142214,#142215,#142216,
#142217,#142218,#142219,#142220,#142221,#142222,#142223,#142224,#142225,
#142226,#142227,#142228,#142229,#142230,#142231,#142232,#142233,#142234,
#142235,#142236,#142237,#142238,#142239,#142240,#142241,#142242,#142243,
#142244,#142245,#142246,#142247,#142248,#142249,#142250,#142251,#142252,
#142253,#142254,#142255,#142256,#142257,#142258,#142259,#142260,#142261,
#142262,#142263,#142264,#142265,#142266,#142267,#142268,#142269,#142270,
#142271,#142272,#142273,#142274,#142275,#142276,#142277,#142278,#142279,
#142280,#142281),.UNSPECIFIED.,.F.,.F.,(4,3,3,3,3,3,3,3,3,3,3,3,3,3,3,3,
3,3,3,3,3,3,3,4),(132.862341310493,132.961797082208,133.060185488697,133.160174943026,
133.260164397355,133.358762522359,133.457220305135,133.557442872908,133.655722430636,
133.753969009709,133.852212092748,133.95390928139,134.052293694809,134.155647271063,
134.259000847317,134.356128675187,134.453094160804,134.549968416923,134.6467826177,
134.743567858739,134.84039997176,134.937256811787,135.034231214226,135.088484104361),
 .UNSPECIFIED.);
#1448=B_SPLINE_CURVE_WITH_KNOTS('',3,(#142282,#142283,#142284,#142285,#142286,
#142287,#142288,#142289),.UNSPECIFIED.,.F.,.F.,(4,1,1,1,1,4),(135.088484104361,
135.257837297279,136.256673747241,137.255510197203,138.254346647165,139.14521341354),
 .UNSPECIFIED.);
#1449=B_SPLINE_CURVE_WITH_KNOTS('',3,(#142295,#142296,#142297,#142298,#142299,
#142300,#142301,#142302,#142303,#142304,#142305,#142306,#142307,#142308,
#142309,#142310,#142311,#142312,#142313,#142314,#142315,#142316,#142317,
#142318,#142319,#142320,#142321,#142322,#142323,#142324,#142325,#142326,
#142327,#142328,#142329,#142330,#142331,#142332,#142333,#142334,#142335,
#142336,#142337,#142338,#142339,#142340,#142341,#142342,#142343,#142344,
#142345,#142346,#142347,#142348,#142349,#142350,#142351,#142352,#142353,
#142354,#142355,#142356,#142357,#142358,#142359,#142360,#142361,#142362,
#142363,#142364,#142365,#142366,#142367,#142368,#142369,#142370,#142371,
#142372,#142373,#142374,#142375,#142376,#142377,#142378,#142379,#142380,
#142381,#142382,#142383,#142384,#142385,#142386,#142387,#142388,#142389,
#142390,#142391,#142392,#142393,#142394,#142395,#142396,#142397,#142398,
#142399,#142400,#142401,#142402,#142403,#142404,#142405,#142406,#142407,
#142408,#142409,#142410,#142411,#142412,#142413,#142414,#142415,#142416,
#142417,#142418),.UNSPECIFIED.,.F.,.F.,(4,3,3,3,3,3,3,3,3,3,3,3,3,3,3,3,
3,3,3,3,3,3,3,3,3,3,3,3,3,3,3,3,3,3,3,3,3,3,3,3,3,4),(141.371669411768,
141.485016004534,141.600339367052,141.71566272957,141.814260854574,141.912718637351,
142.012941205123,142.111220762851,142.209467341925,142.307710424963,142.409407613605,
142.507792027024,142.611145603278,142.714499179532,142.813097304536,142.911555087312,
143.011777655085,143.110057212813,143.208303791887,143.306546874925,143.408244063567,
143.506628476986,143.60998205324,143.713335629494,143.811933754498,143.910391537275,
144.010614105047,144.108893662775,144.207140241849,144.305383324887,144.40708051353,
144.505464926948,144.608818503202,144.712172079456,144.810746601829,144.909191401416,
145.007536191856,145.105810581993,145.204060790382,145.302298022117,145.400579631092,
145.428467355838),.UNSPECIFIED.);
#1450=B_SPLINE_CURVE_WITH_KNOTS('',3,(#142419,#142420,#142421,#142422,#142423,
#142424,#142425,#142426,#142427,#142428,#142429,#142430,#142431,#142432,
#142433,#142434,#142435,#142436,#142437,#142438,#142439,#142440,#142441,
#142442,#142443,#142444,#142445,#142446,#142447,#142448,#142449,#142450,
#142451,#142452,#142453,#142454,#142455,#142456,#142457,#142458,#142459,
#142460,#142461,#142462,#142463,#142464,#142465,#142466,#142467,#142468,
#142469,#142470,#142471,#142472,#142473,#142474,#142475,#142476,#142477,
#142478,#142479,#142480,#142481,#142482,#142483,#142484,#142485,#142486,
#142487,#142488),.UNSPECIFIED.,.F.,.F.,(4,3,3,3,3,3,3,3,3,3,3,3,3,3,3,3,
3,3,3,3,3,3,3,4),(139.146050636314,139.244292899219,139.342541066063,139.440891121064,
139.539292972132,139.637867624459,139.717989829646,139.81658795465,139.915045737426,
140.015268305199,140.113547862927,140.211794442001,140.310037525039,140.411734713681,
140.5101191271,140.613472703354,140.716826279608,140.815569227393,140.914173010821,
141.012667061739,141.111081830931,141.209449097702,141.307822396312,141.371669411541),
 .UNSPECIFIED.);
#1451=B_SPLINE_CURVE_WITH_KNOTS('',3,(#142490,#142491,#142492,#142493,#142494,
#142495,#142496),.UNSPECIFIED.,.F.,.F.,(4,1,1,1,4),(139.14521341354,139.253183097127,
140.252019547089,141.25085599705,141.371669411541),.UNSPECIFIED.);
#1452=B_SPLINE_CURVE_WITH_KNOTS('',3,(#142497,#142498,#142499,#142500,#142501,
#142502,#142503,#142504,#142505,#142506,#142507,#142508,#142509,#142510,
#142511,#142512,#142513,#142514,#142515,#142516,#142517,#142518,#142519,
#142520,#142521,#142522,#142523,#142524,#142525,#142526,#142527,#142528,
#142529,#142530,#142531,#142532,#142533,#142534,#142535,#142536,#142537,
#142538,#142539,#142540,#142541,#142542,#142543,#142544,#142545,#142546,
#142547,#142548,#142549,#142550,#142551,#142552,#142553,#142554,#142555,
#142556,#142557,#142558,#142559,#142560,#142561,#142562,#142563,#142564,
#142565,#142566,#142567,#142568,#142569,#142570,#142571,#142572,#142573,
#142574,#142575,#142576,#142577,#142578,#142579,#142580,#142581,#142582,
#142583,#142584,#142585,#142586,#142587,#142588,#142589,#142590,#142591,
#142592,#142593,#142594,#142595,#142596,#142597,#142598,#142599,#142600,
#142601,#142602,#142603,#142604,#142605,#142606,#142607,#142608,#142609,
#142610,#142611,#142612,#142613,#142614,#142615,#142616,#142617,#142618,
#142619,#142620),.UNSPECIFIED.,.F.,.F.,(4,3,3,3,3,3,3,3,3,3,3,3,3,3,3,3,
3,3,3,3,3,3,3,3,3,3,3,3,3,3,3,3,3,3,3,3,3,3,3,3,3,4),(141.371669411541,
141.468831254161,141.566438903267,141.66339620349,141.760311911022,141.857216996242,
141.955335858935,142.052368429038,142.151030438025,142.249692447012,142.348290572016,
142.446748354792,142.546970922565,142.645250480293,142.743497059367,142.841740142405,
142.943437331047,143.041821744466,143.14517532072,143.248528896974,143.347127021978,
143.445584804755,143.545807372527,143.644086930256,143.742333509329,143.840576592367,
143.94227378101,144.040658194428,144.144011770682,144.247365346936,144.34596347194,
144.444421254716,144.544643822489,144.642923380217,144.741169959291,144.839413042329,
144.941110230971,145.03949464439,145.142848220644,145.246201796898,145.344774861149,
145.429604701798),.UNSPECIFIED.);
#1453=B_SPLINE_CURVE_WITH_KNOTS('',3,(#142626,#142627,#142628,#142629,#142630,
#142631,#142632,#142633,#142634),.UNSPECIFIED.,.F.,.F.,(4,1,1,1,1,1,4),
(147.65485471872,147.708681429341,148.707517879303,149.706354329265,150.705190779227,
151.704027229189,151.712252786696),.UNSPECIFIED.);
#1454=B_SPLINE_CURVE_WITH_KNOTS('',3,(#142635,#142636,#142637,#142638,#142639,
#142640,#142641,#142642,#142643,#142644,#142645,#142646,#142647,#142648,
#142649,#142650,#142651,#142652,#142653,#142654,#142655,#142656,#142657,
#142658,#142659,#142660,#142661,#142662,#142663,#142664,#142665,#142666,
#142667,#142668,#142669,#142670,#142671,#142672,#142673,#142674,#142675,
#142676,#142677,#142678,#142679,#142680,#142681,#142682,#142683,#142684,
#142685,#142686,#142687,#142688,#142689,#142690,#142691,#142692,#142693,
#142694,#142695,#142696,#142697,#142698,#142699,#142700,#142701,#142702,
#142703,#142704),.UNSPECIFIED.,.F.,.F.,(4,3,3,3,3,3,3,3,3,3,3,3,3,3,3,3,
3,3,3,3,3,3,3,4),(145.428467355838,145.526865648701,145.625438470026,145.711008529418,
145.809606654422,145.908064437198,146.008287004971,146.106566562699,146.204813141772,
146.303056224811,146.404753413453,146.503137826872,146.606491403125,146.709844979379,
146.807643480436,146.905302408374,147.002849316603,147.100335701354,147.197792033696,
147.295248746519,147.392798083501,147.490396206244,147.588155506493,147.65485471872),
 .UNSPECIFIED.);
#1455=B_SPLINE_CURVE_WITH_KNOTS('',3,(#142706,#142707,#142708,#142709,#142710,
#142711,#142712,#142713,#142714,#142715,#142716,#142717,#142718,#142719,
#142720,#142721,#142722,#142723,#142724,#142725,#142726,#142727,#142728,
#142729,#142730,#142731,#142732,#142733,#142734,#142735,#142736,#142737,
#142738,#142739,#142740,#142741,#142742,#142743,#142744,#142745,#142746,
#142747,#142748,#142749,#142750,#142751,#142752,#142753,#142754,#142755,
#142756,#142757,#142758,#142759,#142760,#142761,#142762,#142763,#142764,
#142765,#142766,#142767,#142768,#142769,#142770,#142771,#142772,#142773,
#142774,#142775),.UNSPECIFIED.,.F.,.F.,(4,3,3,3,3,3,3,3,3,3,3,3,3,3,3,3,
3,3,3,3,3,3,3,4),(145.429604701798,145.531533894931,145.629819470759,145.728068483142,
145.826310418025,145.924574745627,146.022950495499,146.121392861116,146.219991625193,
146.24503824686,146.343636371864,146.44209415464,146.542316722413,146.640596280141,
146.738842859215,146.837085942253,146.938783130896,147.037167544314,147.140521120568,
147.243874696822,147.352569174392,147.460952550046,147.568802109382,147.654854305401),
 .UNSPECIFIED.);
#1456=B_SPLINE_CURVE_WITH_KNOTS('',3,(#142776,#142777,#142778,#142779,#142780,
#142781,#142782,#142783),.UNSPECIFIED.,.F.,.F.,(4,1,1,1,1,4),(147.65485471872,
148.242711146784,149.241547596745,150.240384046707,151.239220496669,151.712342708042),
 .UNSPECIFIED.);
#1457=B_SPLINE_CURVE_WITH_KNOTS('',3,(#142789,#142790,#142791,#142792,#142793,
#142794,#142795,#142796,#142797,#142798,#142799,#142800,#142801,#142802,
#142803,#142804,#142805,#142806,#142807,#142808,#142809,#142810,#142811,
#142812,#142813,#142814,#142815,#142816,#142817,#142818,#142819,#142820,
#142821,#142822,#142823,#142824,#142825,#142826,#142827,#142828,#142829,
#142830,#142831,#142832,#142833,#142834,#142835,#142836,#142837,#142838,
#142839,#142840,#142841,#142842,#142843,#142844,#142845,#142846,#142847,
#142848,#142849,#142850,#142851,#142852,#142853,#142854,#142855,#142856,
#142857,#142858,#142859,#142860,#142861,#142862,#142863,#142864,#142865,
#142866,#142867,#142868,#142869,#142870,#142871,#142872,#142873,#142874,
#142875,#142876,#142877,#142878,#142879,#142880,#142881,#142882,#142883,
#142884,#142885,#142886,#142887,#142888,#142889,#142890,#142891,#142892,
#142893,#142894,#142895,#142896,#142897,#142898,#142899,#142900,#142901,
#142902,#142903,#142904,#142905,#142906,#142907,#142908,#142909,#142910,
#142911,#142912),.UNSPECIFIED.,.F.,.F.,(4,3,3,3,3,3,3,3,3,3,3,3,3,3,3,3,
3,3,3,3,3,3,3,3,3,3,3,3,3,3,3,3,3,3,3,3,3,3,3,3,3,4),(153.9380400259,154.035163898234,
154.132222574363,154.229246955325,154.326267897773,154.423381488606,154.520541056366,
154.617870832504,154.700536579074,154.799134704076,154.897592486852,154.997815054625,
155.096094612352,155.194341191424,155.292584274461,155.394281463105,155.492665876522,
155.596019452779,155.699373029036,155.797971154037,155.896428936811,155.996651504584,
156.09493106231,156.193177641381,156.291420724416,156.393117913062,156.491502326478,
156.594855902738,156.698209478998,156.796807604012,156.895265386799,156.995487954569,
157.093767512308,157.192014091391,157.29025717444,157.39195436307,157.490338776499,
157.59369235273,157.69704592896,157.795632129846,157.89577062296,157.995909116073),
 .UNSPECIFIED.);
#1458=B_SPLINE_CURVE_WITH_KNOTS('',3,(#142913,#142914,#142915,#142916,#142917,
#142918),.UNSPECIFIED.,.F.,.F.,(4,1,1,4),(151.712252786696,152.702863679151,
153.701700129113,153.93803972631),.UNSPECIFIED.);
#1459=B_SPLINE_CURVE_WITH_KNOTS('',3,(#142920,#142921,#142922,#142923,#142924,
#142925),.UNSPECIFIED.,.F.,.F.,(4,1,1,4),(151.712342708042,152.238056946631,
153.236893396593,153.9380400259),.UNSPECIFIED.);
#1460=B_SPLINE_CURVE_WITH_KNOTS('',3,(#142926,#142927,#142928,#142929,#142930,
#142931,#142932,#142933,#142934,#142935,#142936,#142937,#142938,#142939,
#142940,#142941,#142942,#142943,#142944,#142945,#142946,#142947,#142948,
#142949,#142950,#142951,#142952,#142953,#142954,#142955,#142956,#142957,
#142958,#142959,#142960,#142961,#142962,#142963,#142964,#142965,#142966,
#142967,#142968,#142969,#142970,#142971,#142972,#142973,#142974,#142975,
#142976,#142977,#142978,#142979,#142980,#142981,#142982,#142983,#142984,
#142985,#142986,#142987,#142988,#142989,#142990,#142991,#142992,#142993,
#142994,#142995,#142996,#142997,#142998,#142999,#143000,#143001,#143002,
#143003,#143004,#143005,#143006,#143007,#143008,#143009,#143010,#143011,
#143012,#143013,#143014,#143015,#143016,#143017,#143018,#143019,#143020,
#143021,#143022,#143023,#143024,#143025,#143026,#143027,#143028,#143029,
#143030,#143031,#143032,#143033,#143034,#143035,#143036,#143037,#143038,
#143039,#143040,#143041,#143042,#143043,#143044,#143045,#143046,#143047,
#143048,#143049),.UNSPECIFIED.,.F.,.F.,(4,3,3,3,3,3,3,3,3,3,3,3,3,3,3,3,
3,3,3,3,3,3,3,3,3,3,3,3,3,3,3,3,3,3,3,3,3,3,3,3,3,4),(153.938040202764,
154.056659980231,154.176963650987,154.235729846555,154.334327971559,154.432785754335,
154.533008322108,154.631287879836,154.729534458909,154.827777541948,154.92947473059,
155.027859144009,155.131212720263,155.234566296517,155.33316442152,155.431622204296,
155.531844772069,155.630124329797,155.72837090887,155.826613991908,155.928311180551,
156.026695593969,156.130049170224,156.233402746479,156.332000871484,156.430458654262,
156.530681222034,156.628960779764,156.727207358839,156.825450441878,156.927147630519,
157.025532043939,157.128885620189,157.23223919644,157.33080996438,157.429252216957,
157.527595662266,157.625869905301,157.724128943532,157.822375482216,157.92068828362,
157.994794060844),.UNSPECIFIED.);
#1461=B_SPLINE_CURVE_WITH_KNOTS('',3,(#143055,#143056,#143057,#143058,#143059,
#143060,#143061,#143062),.UNSPECIFIED.,.F.,.F.,(4,1,1,1,1,4),(160.221227414876,
160.693555278846,161.692391728808,162.691228178769,163.690064628731,164.278110108105),
 .UNSPECIFIED.);
#1462=B_SPLINE_CURVE_WITH_KNOTS('',3,(#143063,#143064,#143065,#143066,#143067,
#143068,#143069,#143070,#143071,#143072,#143073,#143074,#143075,#143076,
#143077,#143078,#143079,#143080,#143081,#143082,#143083,#143084,#143085,
#143086,#143087,#143088,#143089,#143090,#143091,#143092,#143093,#143094,
#143095,#143096,#143097,#143098,#143099,#143100,#143101,#143102,#143103,
#143104,#143105,#143106,#143107,#143108,#143109,#143110,#143111,#143112,
#143113,#143114,#143115,#143116,#143117,#143118,#143119,#143120,#143121,
#143122,#143123,#143124,#143125,#143126,#143127,#143128,#143129,#143130,
#143131,#143132),.UNSPECIFIED.,.F.,.F.,(4,3,3,3,3,3,3,3,3,3,3,3,3,3,3,3,
3,3,3,3,3,3,3,4),(157.995909116073,158.094187908191,158.192434197162,158.290677465192,
158.391978693625,158.490363803434,158.593123091178,158.695882378922,158.794480503912,
158.892938286674,158.993160854451,159.091440412165,159.189686991224,159.287930074247,
159.389627262907,159.488011676311,159.591365252598,159.694718828884,159.797216560019,
159.903218753284,160.005303397592,160.107256278837,160.209067828956,160.22122533308),
 .UNSPECIFIED.);
#1463=B_SPLINE_CURVE_WITH_KNOTS('',3,(#143134,#143135,#143136,#143137,#143138,
#143139,#143140,#143141,#143142,#143143,#143144,#143145,#143146,#143147,
#143148,#143149,#143150,#143151,#143152,#143153,#143154,#143155,#143156,
#143157,#143158,#143159,#143160,#143161,#143162,#143163,#143164,#143165,
#143166,#143167,#143168,#143169,#143170,#143171,#143172,#143173,#143174,
#143175,#143176,#143177,#143178,#143179,#143180,#143181,#143182,#143183,
#143184,#143185,#143186,#143187,#143188,#143189,#143190,#143191,#143192,
#143193,#143194,#143195,#143196,#143197,#143198,#143199,#143200,#143201,
#143202,#143203),.UNSPECIFIED.,.F.,.F.,(4,3,3,3,3,3,3,3,3,3,3,3,3,3,3,3,
3,3,3,3,3,3,3,4),(157.994794060844,158.093225180553,158.191816747246,158.231075646402,
158.329673771403,158.428131554177,158.528354121951,158.626633679676,158.724880258747,
158.823123341783,158.924820530428,159.023204943844,159.126558520104,159.229912096364,
159.328378576654,159.426704810661,159.526019875932,159.624169149677,159.722285836342,
159.820399593048,159.920606027993,160.018861091251,160.120043212039,160.221225332828),
 .UNSPECIFIED.);
#1464=B_SPLINE_CURVE_WITH_KNOTS('',3,(#143204,#143205,#143206,#143207,#143208,
#143209,#143210,#143211,#143212,#143213,#143214,#143215,#143216,#143217,
#143218,#143219,#143220,#143221,#143222,#143223,#143224,#143225,#143226,
#143227,#143228,#143229,#143230,#143231,#143232,#143233,#143234,#143235,
#143236,#143237,#143238,#143239,#143240,#143241,#143242,#143243,#143244,
#143245,#143246,#143247,#143248,#143249,#143250,#143251,#143252,#143253,
#143254,#143255,#143256,#143257,#143258,#143259,#143260,#143261,#143262,
#143263,#143264,#143265,#143266,#143267,#143268,#143269,#143270,#143271,
#143272,#143273,#143274,#143275,#143276,#143277,#143278,#143279,#143280,
#143281,#143282,#143283,#143284,#143285,#143286,#143287,#143288,#143289,
#143290,#143291,#143292,#143293,#143294,#143295,#143296,#143297,#143298,
#143299,#143300,#143301,#143302,#143303,#143304,#143305,#143306,#143307,
#143308,#143309,#143310,#143311,#143312,#143313,#143314,#143315,#143316,
#143317,#143318,#143319,#143320,#143321,#143322,#143323,#143324,#143325,
#143326,#143327,#143328,#143329,#143330),.UNSPECIFIED.,.F.,.F.,(4,3,3,3,
3,3,3,3,3,3,3,3,3,3,3,3,3,3,3,3,3,3,3,3,3,3,3,3,3,3,3,3,3,3,3,3,3,3,3,3,
3,3,4),(160.22122533308,160.228748546326,160.327346671318,160.425804454083,
160.526027021859,160.624306579575,160.722553158637,160.820796241665,160.92249343032,
161.020877843728,161.124231420008,161.227584996288,161.326183121278,161.424640904041,
161.524863471817,161.623143029531,161.72138960859,161.819632691614,161.921329880273,
162.019714293678,162.123067869964,162.22642144625,162.325019571326,162.423477354175,
162.52369992193,162.62197947973,162.720226058876,162.818469141986,162.920166330542,
163.018550744032,163.121904320122,163.225257896212,163.323856021116,163.422313803793,
163.522536371591,163.620815929221,163.719062508197,163.817305591139,163.919002779898,
164.017387193223,164.120740769699,164.224094346174,164.278857773673),
 .UNSPECIFIED.);
#1465=B_SPLINE_CURVE_WITH_KNOTS('',3,(#143336,#143337,#143338,#143339,#143340,
#143341,#143342,#143343,#143344,#143345,#143346,#143347,#143348,#143349,
#143350,#143351,#143352,#143353,#143354,#143355,#143356,#143357,#143358,
#143359,#143360,#143361,#143362,#143363,#143364,#143365,#143366,#143367,
#143368,#143369,#143370,#143371,#143372,#143373,#143374,#143375,#143376,
#143377,#143378,#143379,#143380,#143381,#143382,#143383,#143384,#143385,
#143386,#143387,#143388,#143389,#143390,#143391,#143392,#143393,#143394,
#143395,#143396,#143397,#143398,#143399,#143400,#143401,#143402,#143403,
#143404,#143405,#143406,#143407,#143408,#143409,#143410,#143411,#143412,
#143413,#143414,#143415,#143416,#143417,#143418,#143419,#143420,#143421,
#143422,#143423,#143424,#143425,#143426,#143427,#143428,#143429,#143430,
#143431,#143432,#143433,#143434,#143435,#143436,#143437,#143438,#143439,
#143440,#143441,#143442,#143443,#143444,#143445,#143446,#143447,#143448,
#143449,#143450,#143451,#143452,#143453,#143454,#143455,#143456,#143457,
#143458,#143459),.UNSPECIFIED.,.F.,.F.,(4,3,3,3,3,3,3,3,3,3,3,3,3,3,3,3,
3,3,3,3,3,3,3,3,3,3,3,3,3,3,3,3,3,3,3,3,3,3,3,3,3,4),(166.504410640259,
166.652910770224,166.686573978617,166.785172097217,166.883629873595,166.983852442968,
167.082131994357,167.180378567127,167.278621643905,167.380318840074,167.478703247404,
167.582056837991,167.685410428579,167.784008554554,167.882466338243,167.98268890578,
168.080968464273,168.179215044053,168.277458127742,168.379155315442,168.477539729364,
168.580893303952,168.684246878541,168.782845025291,168.881302829915,168.981525392239,
169.079804971904,169.178051572901,169.27629467782,169.377991840491,169.47637627546,
169.579729801982,169.683083328503,169.781689727948,169.880127484655,169.978469449804,
170.076745219915,170.174984320919,170.273261950065,170.371554712618,170.469968413646,
170.561255449419),.UNSPECIFIED.);
#1466=B_SPLINE_CURVE_WITH_KNOTS('',3,(#143460,#143461,#143462,#143463,#143464,
#143465),.UNSPECIFIED.,.F.,.F.,(4,1,1,4),(164.278110108105,164.688901078693,
165.687737528655,166.504405683219),.UNSPECIFIED.);
#1467=B_SPLINE_CURVE_WITH_KNOTS('',3,(#143467,#143468,#143469,#143470,#143471,
#143472,#143473,#143474,#143475,#143476,#143477,#143478,#143479,#143480,
#143481,#143482,#143483,#143484,#143485,#143486,#143487,#143488,#143489,
#143490,#143491,#143492,#143493,#143494,#143495,#143496,#143497,#143498,
#143499,#143500,#143501,#143502,#143503,#143504,#143505,#143506,#143507,
#143508,#143509,#143510,#143511,#143512,#143513,#143514,#143515,#143516,
#143517,#143518,#143519,#143520,#143521,#143522,#143523,#143524,#143525,
#143526,#143527,#143528,#143529,#143530,#143531,#143532,#143533,#143534,
#143535,#143536),.UNSPECIFIED.,.F.,.F.,(4,3,3,3,3,3,3,3,3,3,3,3,3,3,3,3,
3,3,3,3,3,3,3,4),(164.278857773673,164.377373915153,164.475767956526,164.574072829728,
164.672331037576,164.770572077498,164.868825422111,164.967184468132,165.065601061719,
165.164183861903,165.222930796135,165.321528921634,165.419986704907,165.520209272556,
165.618488830781,165.71673541035,165.814978493883,165.916675681936,166.01506009584,
166.118413670969,166.221767246097,166.344599874419,166.465474953174,166.504410639987),
 .UNSPECIFIED.);
#1468=B_SPLINE_CURVE_WITH_KNOTS('',3,(#143537,#143538,#143539,#143540,#143541,
#143542,#143543,#143544,#143545,#143546,#143547,#143548,#143549,#143550,
#143551,#143552,#143553,#143554,#143555,#143556,#143557,#143558,#143559,
#143560,#143561,#143562,#143563,#143564,#143565,#143566,#143567,#143568,
#143569,#143570,#143571,#143572,#143573,#143574,#143575,#143576,#143577,
#143578,#143579,#143580,#143581,#143582,#143583,#143584,#143585,#143586,
#143587,#143588,#143589,#143590,#143591,#143592,#143593,#143594,#143595,
#143596,#143597,#143598,#143599,#143600,#143601,#143602,#143603,#143604,
#143605,#143606,#143607,#143608,#143609,#143610,#143611,#143612,#143613,
#143614,#143615,#143616,#143617,#143618,#143619,#143620,#143621,#143622,
#143623,#143624,#143625,#143626,#143627,#143628,#143629,#143630,#143631,
#143632,#143633,#143634,#143635,#143636,#143637,#143638,#143639,#143640,
#143641,#143642,#143643,#143644,#143645,#143646,#143647,#143648,#143649,
#143650,#143651,#143652,#143653,#143654,#143655,#143656,#143657,#143658,
#143659,#143660,#143661,#143662,#143663),.UNSPECIFIED.,.F.,.F.,(4,3,3,3,
3,3,3,3,3,3,3,3,3,3,3,3,3,3,3,3,3,3,3,3,3,3,3,3,3,3,3,3,3,3,3,3,3,3,3,3,
3,3,4),(166.504410640259,166.6019131263,166.699371433809,166.796815990361,
166.894277201725,166.991846173229,167.089478292238,167.18726953544,167.220603696059,
167.319201820915,167.417659603535,167.517882171346,167.616161728898,167.714408307788,
167.812651390637,167.914348579483,168.012732992698,168.11608656936,168.219440146021,
168.318038274345,168.416496060454,168.516718627395,168.614998188462,168.71324477087,
168.811487857233,168.913185041921,169.011569458608,169.114923027296,169.218276595983,
169.31687471461,169.415332491016,169.515555060382,169.613834611798,169.712081184595,
169.8103242614,169.912021457536,170.010405864893,170.113759455419,170.217113045945,
170.315689889884,170.414143809231,170.512486666529,170.562190685947),
 .UNSPECIFIED.);
#1469=B_SPLINE_CURVE_WITH_KNOTS('',3,(#143669,#143670,#143671,#143672,#143673,
#143674,#143675,#143676,#143677,#143678,#143679,#143680,#143681,#143682,
#143683,#143684,#143685,#143686,#143687,#143688,#143689,#143690,#143691,
#143692,#143693,#143694,#143695,#143696,#143697,#143698,#143699,#143700,
#143701,#143702,#143703,#143704,#143705,#143706,#143707,#143708,#143709,
#143710,#143711,#143712,#143713,#143714,#143715,#143716,#143717,#143718,
#143719,#143720,#143721,#143722,#143723,#143724,#143725,#143726,#143727,
#143728,#143729,#143730,#143731,#143732,#143733,#143734,#143735,#143736,
#143737,#143738,#143739,#143740,#143741,#143742,#143743,#143744,#143745,
#143746,#143747,#143748,#143749,#143750,#143751,#143752,#143753,#143754,
#143755,#143756,#143757,#143758,#143759,#143760,#143761,#143762,#143763,
#143764,#143765,#143766,#143767,#143768,#143769,#143770,#143771,#143772,
#143773,#143774,#143775,#143776,#143777,#143778,#143779,#143780,#143781,
#143782,#143783,#143784,#143785,#143786,#143787,#143788,#143789,#143790,
#143791,#143792,#143793,#143794,#143795),.UNSPECIFIED.,.F.,.F.,(4,3,3,3,
3,3,3,3,3,3,3,3,3,3,3,3,3,3,3,3,3,3,3,3,3,3,3,3,3,3,3,3,3,3,3,3,3,3,3,3,
3,3,4),(172.787595947668,172.884841558621,172.984040004837,173.081071837019,
173.17805926857,173.275033212353,173.375882191352,173.472980624861,173.57014496835,
173.667458405729,173.67842912835,173.777027506528,173.875485539969,173.975708044762,
174.07398784529,174.172234663731,174.270477982414,174.372174881388,174.470559518877,
174.573912548594,174.677265578312,174.775864531657,174.874323148753,174.974545508693,
175.072825909276,175.171073332541,175.26931725999,175.371013452061,175.469398701777,
175.572750365025,175.676102028274,175.774697486027,175.873152598412,175.97337583339,
176.071652732112,176.169896662128,176.268137109468,176.36983745166,176.468219289246,
176.571578883741,176.674938478236,176.773518528001,176.845520779382),
 .UNSPECIFIED.);
#1470=B_SPLINE_CURVE_WITH_KNOTS('',3,(#143796,#143797,#143798,#143799,#143800,
#143801,#143802,#143803,#143804,#143805,#143806,#143807,#143808,#143809,
#143810,#143811,#143812,#143813,#143814,#143815,#143816,#143817,#143818,
#143819,#143820,#143821,#143822,#143823,#143824,#143825,#143826,#143827,
#143828,#143829,#143830,#143831,#143832,#143833,#143834,#143835,#143836,
#143837,#143838,#143839,#143840,#143841,#143842,#143843,#143844,#143845,
#143846,#143847,#143848,#143849,#143850,#143851,#143852,#143853,#143854,
#143855,#143856,#143857,#143858,#143859,#143860,#143861,#143862,#143863,
#143864,#143865),.UNSPECIFIED.,.F.,.F.,(4,3,3,3,3,3,3,3,3,3,3,3,3,3,3,3,
3,3,3,3,3,3,3,4),(170.561255449419,170.659855764701,170.681919778464,170.780517924865,
170.87897572865,170.979198291122,171.077477868766,171.175724467309,171.273967569347,
171.375664734117,171.474049165186,171.577402696806,171.680756228426,171.779354490543,
171.877812411222,171.978034944618,172.076314641176,172.174561359122,172.272804580894,
172.374501605268,172.472886155656,172.576239417022,172.679592678388,172.787595947439),
 .UNSPECIFIED.);
#1471=B_SPLINE_CURVE_WITH_KNOTS('',3,(#143867,#143868,#143869,#143870,#143871,
#143872,#143873,#143874,#143875,#143876,#143877,#143878,#143879,#143880,
#143881,#143882,#143883,#143884,#143885,#143886,#143887,#143888,#143889,
#143890,#143891,#143892,#143893,#143894,#143895,#143896,#143897,#143898,
#143899,#143900,#143901,#143902,#143903,#143904,#143905,#143906,#143907,
#143908,#143909,#143910,#143911,#143912,#143913,#143914,#143915,#143916,
#143917,#143918,#143919,#143920,#143921,#143922,#143923,#143924,#143925,
#143926,#143927,#143928,#143929,#143930,#143931,#143932,#143933,#143934,
#143935,#143936),.UNSPECIFIED.,.F.,.F.,(4,3,3,3,3,3,3,3,3,3,3,3,3,3,3,3,
3,3,3,3,3,3,3,4),(170.562190685947,170.660450522553,170.75869172103,170.856943754601,
170.955300626607,171.053713725501,171.152294519458,171.215949495907,171.314547642559,
171.413005447084,171.513228009432,171.611507588999,171.709754189896,171.807997294717,
171.909694457505,172.008078892377,172.111432419123,172.214785945869,172.31561776535,
172.416285943722,172.516781875652,172.617176498936,172.717484580452,172.787595947439),
 .UNSPECIFIED.);
#1472=B_SPLINE_CURVE_WITH_KNOTS('',3,(#143937,#143938,#143939,#143940,#143941,
#143942,#143943,#143944),.UNSPECIFIED.,.F.,.F.,(4,1,1,1,1,4),(172.787601414666,
173.21362239583,174.212458845792,175.211295295754,176.210131745716,176.844282084543),
 .UNSPECIFIED.);
#1473=B_SPLINE_CURVE_WITH_KNOTS('',3,(#143950,#143951,#143952,#143953,#143954,
#143955,#143956,#143957),.UNSPECIFIED.,.F.,.F.,(4,1,1,1,1,4),(179.070781254618,
179.671447828121,180.670284278083,181.669120728045,182.667957178007,183.128402575235),
 .UNSPECIFIED.);
#1474=B_SPLINE_CURVE_WITH_KNOTS('',3,(#143958,#143959,#143960,#143961,#143962,
#143963,#143964,#143965,#143966,#143967,#143968,#143969,#143970,#143971,
#143972,#143973,#143974,#143975,#143976,#143977,#143978,#143979,#143980,
#143981,#143982,#143983,#143984,#143985,#143986,#143987,#143988,#143989,
#143990,#143991,#143992,#143993,#143994,#143995,#143996,#143997,#143998,
#143999,#144000,#144001,#144002,#144003,#144004,#144005,#144006,#144007,
#144008,#144009,#144010,#144011,#144012,#144013,#144014,#144015,#144016,
#144017,#144018,#144019,#144020,#144021,#144022,#144023,#144024,#144025,
#144026,#144027),.UNSPECIFIED.,.F.,.F.,(4,3,3,3,3,3,3,3,3,3,3,3,3,3,3,3,
3,3,3,3,3,3,3,4),(176.845520779382,176.949052547984,177.047346597006,177.145600689888,
177.243844313097,177.342106934313,177.440479050025,177.538914725845,177.637509924401,
177.673774928198,177.772377764237,177.87084030234,177.971061686817,178.069346073264,
178.167597497761,178.265845436446,178.367536921874,178.465926166336,178.569268772248,
178.672611378159,178.782250112465,178.89154546425,179.000249342496,179.070781030154),
 .UNSPECIFIED.);
#1475=B_SPLINE_CURVE_WITH_KNOTS('',3,(#144029,#144030,#144031,#144032,#144033,
#144034),.UNSPECIFIED.,.F.,.F.,(4,1,1,4),(176.844282084543,177.208968195678,
178.20780464564,179.070781254618),.UNSPECIFIED.);
#1476=B_SPLINE_CURVE_WITH_KNOTS('',3,(#144035,#144036,#144037,#144038,#144039,
#144040,#144041,#144042),.UNSPECIFIED.,.F.,.F.,(4,1,1,1,1,4),(179.070781254618,
179.206641095602,180.205477545564,181.204313995525,182.203150445487,183.127688309466),
 .UNSPECIFIED.);
#1477=B_SPLINE_CURVE_WITH_KNOTS('',3,(#144048,#144049,#144050,#144051,#144052,
#144053,#144054,#144055),.UNSPECIFIED.,.F.,.F.,(4,1,1,1,1,4),(15.707963267949,
15.8622700343739,16.8611064843358,17.8599429342977,18.8587793842596,19.7647623411309),
 .UNSPECIFIED.);
#1478=B_SPLINE_CURVE_WITH_KNOTS('',3,(#144057,#144058,#144059,#144060,#144061,
#144062,#144063,#144064,#144065,#144066,#144067,#144068,#144069,#144070,
#144071,#144072,#144073,#144074,#144075,#144076,#144077,#144078,#144079,
#144080,#144081,#144082,#144083,#144084,#144085,#144086,#144087,#144088,
#144089,#144090,#144091,#144092,#144093,#144094,#144095,#144096,#144097,
#144098,#144099,#144100,#144101,#144102,#144103,#144104,#144105,#144106,
#144107,#144108,#144109,#144110,#144111,#144112,#144113,#144114),
 .UNSPECIFIED.,.F.,.F.,(4,3,3,3,3,3,3,3,3,3,3,3,3,3,3,3,3,3,3,4),(13.8757070305517,
13.9742335889647,14.072619844817,14.1714715622663,14.2696802945035,14.3678559192405,
14.4660280130677,14.5653794059038,14.6636894122209,14.7635614983165,14.8634335844121,
14.9606976622509,15.0578044027615,15.1548229002686,15.2517842042296,15.3487192914879,
15.4457083558909,15.5427241566488,15.6398692495935,15.707963267949),
 .UNSPECIFIED.);
#1479=B_SPLINE_CURVE_WITH_KNOTS('',3,(#144118,#144119,#144120,#144121,#144122),
 .UNSPECIFIED.,.F.,.F.,(4,1,4),(14.3986268518925,15.3974633018543,15.707963267949),
 .UNSPECIFIED.);
#1480=B_SPLINE_CURVE_WITH_KNOTS('',3,(#144123,#144124,#144125,#144126,#144127,
#144128,#144129,#144130),.UNSPECIFIED.,.F.,.F.,(4,1,1,1,1,4),(15.707963267949,
16.3962997518162,17.3951362017781,18.39397265174,19.3928091017018,19.7659327876261),
 .UNSPECIFIED.);
#1481=B_SPLINE_CURVE_WITH_KNOTS('',3,(#144136,#144137,#144138,#144139,#144140,
#144141,#144142,#144143),.UNSPECIFIED.,.F.,.F.,(4,1,1,1,1,4),(21.9911485751286,
22.854125184107,23.8529616340689,24.8517980840308,25.8506345339927,26.0493850773176),
 .UNSPECIFIED.);
#1482=B_SPLINE_CURVE_WITH_KNOTS('',3,(#144144,#144145,#144146,#144147,#144148,
#144149,#144150),.UNSPECIFIED.,.F.,.F.,(4,1,1,1,4),(19.7647623411309,19.8576158342214,
20.8564522841833,21.8552887341452,21.9911485751286),.UNSPECIFIED.);
#1483=B_SPLINE_CURVE_WITH_KNOTS('',3,(#144152,#144153,#144154,#144155,#144156,
#144157),.UNSPECIFIED.,.F.,.F.,(4,1,1,4),(19.7659327876261,20.3916455516637,
21.3904820016256,21.9911485751286),.UNSPECIFIED.);
#1484=B_SPLINE_CURVE_WITH_KNOTS('',3,(#144158,#144159,#144160,#144161,#144162,
#144163,#144164,#144165,#144166,#144167,#144168,#144169,#144170,#144171,
#144172,#144173,#144174,#144175,#144176,#144177,#144178,#144179,#144180,
#144181,#144182,#144183,#144184,#144185,#144186,#144187,#144188,#144189,
#144190,#144191,#144192,#144193,#144194,#144195,#144196,#144197,#144198,
#144199,#144200,#144201,#144202,#144203,#144204,#144205,#144206,#144207,
#144208,#144209,#144210,#144211,#144212,#144213,#144214,#144215,#144216,
#144217,#144218,#144219,#144220,#144221,#144222,#144223,#144224,#144225,
#144226,#144227,#144228,#144229,#144230,#144231,#144232,#144233,#144234,
#144235,#144236,#144237,#144238,#144239,#144240,#144241,#144242,#144243,
#144244,#144245,#144246,#144247,#144248,#144249,#144250,#144251,#144252,
#144253,#144254,#144255,#144256,#144257,#144258,#144259,#144260,#144261,
#144262,#144263,#144264,#144265,#144266,#144267,#144268,#144269,#144270,
#144271,#144272,#144273,#144274,#144275,#144276,#144277,#144278,#144279,
#144280,#144281),.UNSPECIFIED.,.F.,.F.,(4,3,3,3,3,3,3,3,3,3,3,3,3,3,3,3,
3,3,3,3,3,3,3,3,3,3,3,3,3,3,3,3,3,3,3,3,3,3,3,3,3,4),(21.9911487995816,
22.0999040743052,22.2090426220591,22.3187161819304,22.3893184515875,22.487921325434,
22.5863838904609,22.6866052668469,22.7848896533628,22.8831410679294,22.9813889867089,
23.083080465419,23.1814696653607,23.284812283455,23.3881549015493,23.4867551946089,
23.5852151974108,23.6854372166734,23.7837191063733,23.8819680542081,23.9802135397836,
24.0819079927155,24.180294868899,24.2836431102051,24.3869913515112,24.4855869800636,
24.5840422282252,24.6842654248812,24.7825423726193,24.8807863192412,24.9790267507949,
25.0807270134645,25.1791087548176,25.2824682781454,25.3858278014731,25.4844081039851,
25.5828572783489,25.6812050438807,25.779488016792,25.8777310255654,25.9759959055665,
26.0480412392441),.UNSPECIFIED.);
#1485=B_SPLINE_CURVE_WITH_KNOTS('',3,(#144287,#144288,#144289,#144290,#144291,
#144292,#144293,#144294,#144295,#144296,#144297,#144298,#144299,#144300,
#144301,#144302,#144303,#144304,#144305,#144306,#144307,#144308,#144309,
#144310,#144311,#144312,#144313,#144314,#144315,#144316,#144317,#144318,
#144319,#144320,#144321,#144322,#144323,#144324,#144325,#144326,#144327,
#144328,#144329,#144330,#144331,#144332,#144333,#144334,#144335,#144336,
#144337,#144338,#144339,#144340,#144341,#144342,#144343,#144344,#144345,
#144346,#144347,#144348,#144349,#144350,#144351,#144352,#144353,#144354,
#144355,#144356,#144357,#144358,#144359,#144360,#144361,#144362,#144363,
#144364,#144365,#144366,#144367,#144368,#144369,#144370,#144371,#144372,
#144373,#144374,#144375,#144376,#144377,#144378,#144379,#144380,#144381,
#144382,#144383,#144384,#144385,#144386,#144387,#144388,#144389,#144390,
#144391,#144392,#144393,#144394,#144395,#144396,#144397,#144398,#144399,
#144400,#144401,#144402,#144403,#144404,#144405,#144406,#144407,#144408,
#144409,#144410),.UNSPECIFIED.,.F.,.F.,(4,3,3,3,3,3,3,3,3,3,3,3,3,3,3,3,
3,3,3,3,3,3,3,3,3,3,3,3,3,3,3,3,3,3,3,3,3,3,3,3,3,4),(28.2743338823082,
28.3746245106346,28.4749734038757,28.575488632026,28.6760922702813,28.7769068624063,
28.8471438838783,28.9457420299521,29.0441998340445,29.144422396519,29.2427019760092,
29.3409485769638,29.4391916819739,29.5408888449405,29.6392732803314,29.7426268070858,
29.8459803338402,29.9445784592259,30.043036242451,30.1432588101199,30.241538368458,
30.3397849482006,30.4380280319667,30.5397252199255,30.6381096342119,30.7414632090069,
30.844816783802,30.9434149029147,31.041872679697,31.1420952489554,31.240374800478,
31.3386213732805,31.4368644499908,31.5385616459341,31.6369460529461,31.740299643355,
31.8436532337639,31.9422528703149,32.0406907036705,32.1390337581153,32.237318176998,
32.3317147986234),.UNSPECIFIED.);
#1486=B_SPLINE_CURVE_WITH_KNOTS('',3,(#144411,#144412,#144413,#144414,#144415,
#144416),.UNSPECIFIED.,.F.,.F.,(4,1,1,4),(26.0493850773176,26.8494709839545,
27.8483074339164,28.2743284148014),.UNSPECIFIED.);
#1487=B_SPLINE_CURVE_WITH_KNOTS('',3,(#144418,#144419,#144420,#144421,#144422,
#144423,#144424,#144425,#144426,#144427,#144428,#144429,#144430,#144431,
#144432,#144433,#144434,#144435,#144436,#144437,#144438,#144439,#144440,
#144441,#144442,#144443,#144444,#144445,#144446,#144447,#144448,#144449,
#144450,#144451,#144452,#144453,#144454,#144455,#144456,#144457,#144458,
#144459,#144460,#144461,#144462,#144463,#144464,#144465,#144466,#144467,
#144468,#144469,#144470,#144471,#144472,#144473,#144474,#144475,#144476,
#144477,#144478,#144479,#144480,#144481,#144482,#144483,#144484,#144485,
#144486,#144487,#144488,#144489,#144490),.UNSPECIFIED.,.F.,.F.,(4,3,3,3,
3,3,3,3,3,3,3,3,3,3,3,3,3,3,3,3,3,3,3,3,4),(26.0480412392441,26.1464094161118,
26.2448398501594,26.3434312965433,26.384664251435,26.4832625888131,26.5817205900565,
26.681943103974,26.780222893609,26.8784697091132,26.9767130328096,27.0784099499564,
27.1767946121896,27.2801476567932,27.3835007013968,27.4808124356152,27.5800026164232,
27.6770619121749,27.7740624149263,27.8710350587886,27.9718597646113,28.0689211634457,
28.1660361050485,28.2632831532614,28.2743338820794),.UNSPECIFIED.);
#1488=B_SPLINE_CURVE_WITH_KNOTS('',3,(#144491,#144492,#144493,#144494,#144495,
#144496,#144497,#144498,#144499,#144500,#144501,#144502,#144503,#144504,
#144505,#144506,#144507,#144508,#144509,#144510,#144511,#144512,#144513,
#144514,#144515,#144516,#144517,#144518,#144519,#144520,#144521,#144522,
#144523,#144524,#144525,#144526,#144527,#144528,#144529,#144530,#144531,
#144532,#144533,#144534,#144535,#144536,#144537,#144538,#144539,#144540,
#144541,#144542,#144543,#144544,#144545,#144546,#144547,#144548,#144549,
#144550,#144551,#144552,#144553,#144554,#144555,#144556,#144557,#144558,
#144559,#144560,#144561,#144562,#144563,#144564,#144565,#144566,#144567,
#144568,#144569,#144570,#144571,#144572,#144573,#144574,#144575,#144576,
#144577,#144578,#144579,#144580,#144581,#144582,#144583,#144584,#144585,
#144586,#144587,#144588,#144589,#144590,#144591,#144592,#144593,#144594,
#144595,#144596,#144597,#144598,#144599,#144600,#144601,#144602,#144603,
#144604,#144605,#144606,#144607,#144608,#144609,#144610,#144611,#144612,
#144613,#144614),.UNSPECIFIED.,.F.,.F.,(4,3,3,3,3,3,3,3,3,3,3,3,3,3,3,3,
3,3,3,3,3,3,3,3,3,3,3,3,3,3,3,3,3,3,3,3,3,3,3,3,3,4),(28.2743338823082,
28.3823371513587,28.4809354100483,28.5793933279209,28.6796158620959,28.7778955573906,
28.876142274651,28.9743854963144,29.0760825225659,29.1744670742836,29.2778203378021,
29.3811736013206,29.47977174272,29.5782295425626,29.6784521061526,29.7767316824779,
29.8749782806812,29.9732213833592,30.07491855034,30.173302984478,30.2766565178803,
30.3800100512825,30.4786081310757,30.5770658678857,30.6772884470555,30.7755679572915,
30.8738144884062,30.9720575230819,31.0737547676225,31.1721391321597,31.275492816702,
31.3788465012443,31.4774477473466,31.5759078066679,31.6742504131212,31.7725287579753,
31.8707723649116,31.9690107165623,32.0673303010146,32.1656922450024,32.2642027659188,
32.3314303507724),.UNSPECIFIED.);
#1489=B_SPLINE_CURVE_WITH_KNOTS('',3,(#144620,#144621,#144622,#144623,#144624,
#144625,#144626,#144627,#144628,#144629,#144630,#144631,#144632,#144633,
#144634,#144635,#144636,#144637,#144638,#144639,#144640,#144641,#144642,
#144643,#144644,#144645,#144646,#144647,#144648,#144649,#144650,#144651,
#144652,#144653,#144654,#144655,#144656,#144657,#144658,#144659,#144660,
#144661,#144662,#144663,#144664,#144665,#144666,#144667,#144668,#144669,
#144670,#144671,#144672,#144673,#144674,#144675,#144676,#144677,#144678,
#144679,#144680,#144681,#144682,#144683,#144684,#144685,#144686,#144687,
#144688,#144689,#144690,#144691,#144692,#144693,#144694,#144695,#144696,
#144697,#144698,#144699,#144700,#144701,#144702,#144703,#144704,#144705,
#144706,#144707,#144708,#144709,#144710,#144711,#144712,#144713,#144714,
#144715,#144716,#144717,#144718,#144719,#144720,#144721,#144722,#144723,
#144724,#144725,#144726,#144727,#144728,#144729,#144730,#144731,#144732,
#144733,#144734,#144735,#144736,#144737,#144738,#144739,#144740,#144741,
#144742,#144743),.UNSPECIFIED.,.F.,.F.,(4,3,3,3,3,3,3,3,3,3,3,3,3,3,3,3,
3,3,3,3,3,3,3,3,3,3,3,3,3,3,3,3,3,3,3,3,3,3,3,3,3,4),(34.5575191897594,
34.6782345503608,34.8009387396036,34.8401625836495,34.9387607091287,35.0372184923873,
35.1374410600403,35.2357206182623,35.333967197833,35.4322102813716,35.5339074694315,
35.6322918833522,35.7356454584818,35.8389990336114,35.9375971585481,36.0360549412581,
36.1362775090475,36.2345570667098,36.3328036457177,36.4310467286914,36.5327439174119,
36.6311283307679,36.7344819071706,36.8378354835733,36.9364336084865,37.034891391171,
37.1351139589665,37.2333935165987,37.3316400955748,37.429883178515,37.5315803672701,
37.6299647805889,37.7333183570621,37.8366719335352,37.9352415778349,38.0336830992393,
38.1320262040969,38.2303004962056,38.328562793654,38.4268127465216,38.5251372404807,
38.6142676624748),.UNSPECIFIED.);
#1490=B_SPLINE_CURVE_WITH_KNOTS('',3,(#144744,#144745,#144746,#144747,#144748,
#144749,#144750,#144751,#144752,#144753,#144754,#144755,#144756,#144757,
#144758,#144759,#144760,#144761,#144762,#144763,#144764,#144765,#144766,
#144767,#144768,#144769,#144770,#144771,#144772,#144773,#144774,#144775,
#144776,#144777,#144778,#144779,#144780,#144781,#144782,#144783,#144784,
#144785,#144786,#144787,#144788,#144789,#144790,#144791,#144792,#144793,
#144794,#144795,#144796,#144797,#144798,#144799,#144800,#144801,#144802,
#144803,#144804,#144805,#144806,#144807,#144808,#144809,#144810,#144811,
#144812,#144813,#144814,#144815,#144816),.UNSPECIFIED.,.F.,.F.,(4,3,3,3,
3,3,3,3,3,3,3,3,3,3,3,3,3,3,3,3,3,3,3,3,4),(32.3317147986234,32.4299572783543,
32.5330903796972,32.6314723034345,32.7299238260328,32.8285286780479,32.8424896837258,
32.9410878085144,33.0395455910817,33.1397681589074,33.2380477164404,33.3362942953245,
33.4345373781799,33.5362345670569,33.6346189803101,33.7379725569989,33.8413261336877,
33.93909739415,34.0367388270534,34.1342810926871,34.2317547370018,34.3292101035708,
34.426655495324,34.5241539308998,34.5575191894878),.UNSPECIFIED.);
#1491=B_SPLINE_CURVE_WITH_KNOTS('',3,(#144818,#144819,#144820,#144821,#144822,
#144823,#144824,#144825,#144826,#144827,#144828,#144829,#144830,#144831,
#144832,#144833,#144834,#144835,#144836,#144837,#144838,#144839,#144840,
#144841,#144842,#144843,#144844,#144845,#144846,#144847,#144848,#144849,
#144850,#144851,#144852,#144853,#144854,#144855,#144856,#144857,#144858,
#144859,#144860,#144861,#144862,#144863,#144864,#144865,#144866,#144867,
#144868,#144869,#144870,#144871,#144872,#144873,#144874,#144875,#144876,
#144877,#144878,#144879,#144880,#144881,#144882,#144883,#144884,#144885,
#144886,#144887),.UNSPECIFIED.,.F.,.F.,(4,3,3,3,3,3,3,3,3,3,3,3,3,3,3,3,
3,3,3,3,3,3,3,4),(32.3314303507724,32.3776829512062,32.4762810765969,32.5747388598271,
32.6749614274947,32.7732409858373,32.871487565584,32.9697306493543,33.0714278373078,
33.1698122515977,33.2731658263829,33.3765194011681,33.4751175203039,33.5735752971096,
33.6737978663622,33.7720774179092,33.8703239907363,33.9685670674716,34.0702642633862,
34.1686486704234,34.2720022607767,34.37535585113,34.5238559809678,34.5575191894878),
 .UNSPECIFIED.);
#1492=B_SPLINE_CURVE_WITH_KNOTS('',3,(#144888,#144889,#144890,#144891,#144892,
#144893,#144894,#144895),.UNSPECIFIED.,.F.,.F.,(4,1,1,1,1,4),(34.5575241471828,
35.3741923010918,36.3730287510537,37.3718652010156,38.3707016509774,38.6157831659124),
 .UNSPECIFIED.);
#1493=B_SPLINE_CURVE_WITH_KNOTS('',3,(#144901,#144902,#144903,#144904,#144905,
#144906,#144907,#144908,#144909,#144910,#144911,#144912,#144913,#144914,
#144915,#144916,#144917,#144918,#144919,#144920,#144921,#144922,#144923,
#144924,#144925,#144926,#144927,#144928,#144929,#144930,#144931,#144932,
#144933,#144934,#144935,#144936,#144937,#144938,#144939,#144940,#144941,
#144942,#144943,#144944,#144945,#144946,#144947,#144948,#144949,#144950,
#144951,#144952,#144953,#144954,#144955,#144956,#144957,#144958,#144959,
#144960,#144961,#144962,#144963,#144964,#144965,#144966,#144967,#144968,
#144969,#144970,#144971,#144972,#144973,#144974,#144975,#144976,#144977,
#144978,#144979,#144980,#144981,#144982,#144983,#144984,#144985,#144986,
#144987,#144988,#144989,#144990,#144991,#144992,#144993,#144994,#144995,
#144996,#144997,#144998,#144999,#145000,#145001,#145002,#145003,#145004,
#145005,#145006,#145007,#145008,#145009,#145010,#145011,#145012,#145013,
#145014,#145015,#145016,#145017,#145018,#145019,#145020,#145021,#145022,
#145023,#145024),.UNSPECIFIED.,.F.,.F.,(4,3,3,3,3,3,3,3,3,3,3,3,3,3,3,3,
3,3,3,3,3,3,3,3,3,3,3,3,3,3,3,3,3,3,3,3,3,3,3,3,3,4),(40.8407044969197,
40.9391705387199,41.0374964280042,41.1368115911765,41.2349607512895,41.3330774110131,
41.4311912274066,41.5313978539006,41.6296531901077,41.7308354617452,41.8320177333827,
41.9306158583837,42.0290736411578,42.1292962089311,42.2275757666566,42.3258223457272,
42.424065428763,42.5257626174084,42.6241470308244,42.7275006070845,42.8308541833445,
42.929452308347,43.0279100911226,43.1281326588956,43.2264122166225,43.3246587956946,
43.4229018787317,43.5245990673754,43.6229834807929,43.7263370570496,43.8296906333064,
43.9282887583114,44.0267465410897,44.126969108862,44.2252486665916,44.3234952456665,
44.4217383287062,44.5234355173468,44.6218199307671,44.7251735070177,44.8285270832683,
44.8983979680182),.UNSPECIFIED.);
#1494=B_SPLINE_CURVE_WITH_KNOTS('',3,(#145025,#145026,#145027,#145028,#145029,
#145030,#145031,#145032,#145033,#145034,#145035,#145036,#145037,#145038,
#145039,#145040,#145041,#145042,#145043,#145044,#145045,#145046,#145047,
#145048,#145049,#145050,#145051,#145052,#145053,#145054,#145055,#145056,
#145057,#145058,#145059,#145060,#145061,#145062,#145063,#145064,#145065,
#145066,#145067,#145068,#145069,#145070,#145071,#145072,#145073,#145074,
#145075,#145076,#145077,#145078,#145079,#145080,#145081,#145082,#145083,
#145084,#145085,#145086,#145087,#145088,#145089,#145090,#145091,#145092,
#145093,#145094,#145095,#145096,#145097),.UNSPECIFIED.,.F.,.F.,(4,3,3,3,
3,3,3,3,3,3,3,3,3,3,3,3,3,3,3,3,3,3,3,3,4),(38.6142676624748,38.7127107166971,
38.8113099318161,38.835508383497,38.9341065084864,39.0325642912487,39.132786859025,
39.2310664167387,39.3293129957976,39.4275560788218,39.5292532674811,39.6276376808857,
39.7309912571723,39.8343448334589,39.9329429584521,40.0314007412181,40.1316233089935,
40.2299028667104,40.3281494457725,40.4263925287994,40.5280897174548,40.6264741308618,
40.7298277071413,40.8331812834208,40.8407044966674),.UNSPECIFIED.);
#1495=B_SPLINE_CURVE_WITH_KNOTS('',3,(#145099,#145100,#145101,#145102,#145103,
#145104),.UNSPECIFIED.,.F.,.F.,(4,1,1,4),(38.6157831659124,39.3695381009393,
40.3683745509012,40.8407024149584),.UNSPECIFIED.);
#1496=B_SPLINE_CURVE_WITH_KNOTS('',3,(#145105,#145106,#145107,#145108,#145109,
#145110,#145111,#145112,#145113,#145114,#145115,#145116,#145117,#145118,
#145119,#145120,#145121,#145122,#145123,#145124,#145125,#145126,#145127,
#145128,#145129,#145130,#145131,#145132,#145133,#145134,#145135,#145136,
#145137,#145138,#145139,#145140,#145141,#145142,#145143,#145144,#145145,
#145146,#145147,#145148,#145149,#145150,#145151,#145152,#145153,#145154,
#145155,#145156,#145157,#145158,#145159,#145160,#145161,#145162,#145163,
#145164,#145165,#145166,#145167,#145168,#145169,#145170,#145171,#145172,
#145173,#145174,#145175,#145176,#145177,#145178,#145179,#145180,#145181,
#145182,#145183,#145184,#145185,#145186,#145187,#145188,#145189,#145190,
#145191,#145192,#145193,#145194,#145195,#145196,#145197,#145198,#145199,
#145200,#145201,#145202,#145203,#145204,#145205,#145206,#145207,#145208,
#145209,#145210,#145211,#145212,#145213,#145214,#145215,#145216,#145217,
#145218,#145219,#145220,#145221,#145222,#145223,#145224,#145225,#145226,
#145227,#145228,#145229,#145230,#145231),.UNSPECIFIED.,.F.,.F.,(4,3,3,3,
3,3,3,3,3,3,3,3,3,3,3,3,3,3,3,3,3,3,3,3,3,3,3,3,3,3,3,3,3,3,3,3,3,3,3,3,
3,3,4),(40.8407044966674,40.9425310419931,41.0487010317106,41.1508691915794,
41.2531658485544,41.3556785603232,41.3672110008631,41.4658091258525,41.5642669086152,
41.6644894763914,41.7627690341051,41.8610156131641,41.9592586961883,42.0609558848474,
42.1593402982521,42.2626938745385,42.3660474508249,42.4646455758182,42.5631033585842,
42.6633259263595,42.7616054840765,42.8598520631385,42.9580951461655,43.0597923348208,
43.1581767482279,43.2615303245073,43.3648839007868,43.4634820258002,43.5619398085867,
43.6621623763569,43.7604419340952,43.8586885131787,43.9569315962273,44.0586287848577,
44.157013198287,44.2603667745178,44.3637203507487,44.4623140220524,44.5607732131559,
44.6591152246758,44.757389474878,44.8556332863474,44.8979423039439),
 .UNSPECIFIED.);
#1497=B_SPLINE_CURVE_WITH_KNOTS('',3,(#145237,#145238,#145239,#145240,#145241,
#145242,#145243,#145244),.UNSPECIFIED.,.F.,.F.,(4,1,1,1,1,4),(47.123889803847,
47.8250364331539,48.8238728831158,49.8227093330777,50.8215457830395,51.1819114029981),
 .UNSPECIFIED.);
#1498=B_SPLINE_CURVE_WITH_KNOTS('',3,(#145245,#145246,#145247,#145248,#145249,
#145250,#145251,#145252,#145253,#145254,#145255,#145256,#145257,#145258,
#145259,#145260,#145261,#145262,#145263,#145264,#145265,#145266,#145267,
#145268,#145269,#145270,#145271,#145272,#145273,#145274,#145275,#145276,
#145277,#145278,#145279,#145280,#145281,#145282,#145283,#145284,#145285,
#145286,#145287,#145288,#145289,#145290,#145291,#145292,#145293,#145294,
#145295,#145296,#145297,#145298,#145299,#145300,#145301,#145302,#145303,
#145304,#145305,#145306,#145307,#145308,#145309,#145310,#145311,#145312,
#145313,#145314),.UNSPECIFIED.,.F.,.F.,(4,3,3,3,3,3,3,3,3,3,3,3,3,3,3,3,
3,3,3,3,3,3,3,4),(44.8983979680182,44.9968932668749,45.0952714925266,45.1935672979277,
45.2918209615386,45.3900619752629,45.4883198102566,45.5866859517105,45.6851137001938,
45.7837031754335,45.8273635332302,45.9259616582337,46.0244194410101,46.1246420087828,
46.2229215665108,46.3211681455839,46.4194112286225,46.5211084172648,46.6194928306836,
46.7228464069378,46.826199983192,46.9466622822351,47.0654828012647,47.1238896269613),
 .UNSPECIFIED.);
#1499=B_SPLINE_CURVE_WITH_KNOTS('',3,(#145316,#145317,#145318,#145319,#145320,
#145321,#145322,#145323,#145324,#145325,#145326,#145327,#145328,#145329,
#145330,#145331,#145332,#145333,#145334,#145335,#145336,#145337,#145338,
#145339,#145340,#145341,#145342,#145343,#145344,#145345,#145346,#145347,
#145348,#145349,#145350,#145351,#145352,#145353,#145354,#145355,#145356,
#145357,#145358,#145359,#145360,#145361,#145362,#145363,#145364,#145365,
#145366,#145367,#145368,#145369,#145370,#145371,#145372,#145373,#145374,
#145375,#145376,#145377,#145378,#145379,#145380,#145381,#145382,#145383,
#145384,#145385),.UNSPECIFIED.,.F.,.F.,(4,3,3,3,3,3,3,3,3,3,3,3,3,3,3,3,
3,3,3,3,3,3,3,4),(44.8979423039439,44.9961925047522,45.0945462342209,45.1929542076481,
45.2915321400895,45.3625568007106,45.4611549257133,45.5596127084887,45.6598352762617,
45.7581148339886,45.8563614130606,45.9546044960977,46.0563016847413,46.1546860981589,
46.2580396744156,46.3613932506724,46.4587199838046,46.5559210250953,46.6530274701202,
46.7500702965176,46.8471124553619,46.9441490048062,47.0412721236582,47.123889803847),
 .UNSPECIFIED.);
#1500=B_SPLINE_CURVE_WITH_KNOTS('',3,(#145386,#145387,#145388,#145389,#145390,
#145391,#145392,#145393),.UNSPECIFIED.,.F.,.F.,(4,1,1,1,1,4),(47.1238901028405,
47.3602297006343,48.3590661505962,49.3579026005581,50.3567390505199,51.180388194529),
 .UNSPECIFIED.);
#1501=B_SPLINE_CURVE_WITH_KNOTS('',3,(#145399,#145400,#145401,#145402,#145403,
#145404,#145405,#145406,#145407,#145408,#145409,#145410,#145411,#145412,
#145413,#145414,#145415,#145416,#145417,#145418,#145419,#145420,#145421,
#145422,#145423,#145424,#145425,#145426,#145427,#145428,#145429,#145430,
#145431,#145432,#145433,#145434,#145435,#145436,#145437,#145438,#145439,
#145440,#145441,#145442,#145443,#145444,#145445,#145446,#145447,#145448,
#145449,#145450,#145451,#145452,#145453,#145454,#145455,#145456,#145457,
#145458,#145459,#145460,#145461,#145462,#145463,#145464,#145465,#145466,
#145467,#145468,#145469,#145470,#145471,#145472,#145473,#145474,#145475,
#145476,#145477,#145478,#145479,#145480,#145481,#145482,#145483,#145484,
#145485,#145486,#145487,#145488,#145489,#145490,#145491,#145492,#145493,
#145494,#145495,#145496,#145497,#145498,#145499,#145500,#145501,#145502,
#145503,#145504,#145505,#145506,#145507,#145508,#145509,#145510,#145511,
#145512,#145513,#145514,#145515,#145516,#145517,#145518,#145519,#145520,
#145521,#145522),.UNSPECIFIED.,.F.,.F.,(4,3,3,3,3,3,3,3,3,3,3,3,3,3,3,3,
3,3,3,3,3,3,3,3,3,3,3,3,3,3,3,3,3,3,3,3,3,3,3,3,3,4),(53.4070755243676,
53.5149520672777,53.623163861073,53.7318758460237,53.8180551329252,53.9166532579289,
54.0151110407056,54.1153336084783,54.2136131662064,54.3118597452797,54.4101028283182,
54.5118000169604,54.6101844303791,54.7135380066331,54.816891582887,54.9154897078907,
55.0139474906675,55.1141700584402,55.2124496161683,55.3106961952417,55.4089392782802,
55.5106364669224,55.6090208803412,55.7123744565951,55.8157280328489,55.9143261578526,
56.0127839406294,56.113006508402,56.2112860661302,56.3095326452036,56.4077757282421,
56.5094729168843,56.6078573303031,56.7112109065569,56.8145644828108,56.9131452274569,
57.0115945031609,57.1099420320499,57.2082227592529,57.3064633876105,57.4047205556915,
57.4639959741701),.UNSPECIFIED.);
#1502=B_SPLINE_CURVE_WITH_KNOTS('',3,(#145523,#145524,#145525,#145526,#145527,
#145528),.UNSPECIFIED.,.F.,.F.,(4,1,1,4),(51.1819114029981,51.8203822330014,
52.8192186829633,53.4070751110266),.UNSPECIFIED.);
#1503=B_SPLINE_CURVE_WITH_KNOTS('',3,(#145530,#145531,#145532,#145533,#145534,
#145535,#145536),.UNSPECIFIED.,.F.,.F.,(4,1,1,1,4),(51.180388194529,51.3555755004818,
52.3544119504437,53.3532484004056,53.4070751110266),.UNSPECIFIED.);
#1504=B_SPLINE_CURVE_WITH_KNOTS('',3,(#145537,#145538,#145539,#145540,#145541,
#145542,#145543,#145544,#145545,#145546,#145547,#145548,#145549,#145550,
#145551,#145552,#145553,#145554,#145555,#145556,#145557,#145558,#145559,
#145560,#145561,#145562,#145563,#145564,#145565,#145566,#145567,#145568,
#145569,#145570,#145571,#145572,#145573,#145574,#145575,#145576,#145577,
#145578,#145579,#145580,#145581,#145582,#145583,#145584,#145585,#145586,
#145587,#145588,#145589,#145590,#145591,#145592,#145593,#145594,#145595,
#145596,#145597,#145598,#145599,#145600,#145601,#145602,#145603,#145604,
#145605,#145606,#145607,#145608,#145609,#145610,#145611,#145612,#145613,
#145614,#145615,#145616,#145617,#145618,#145619,#145620,#145621,#145622,
#145623,#145624,#145625,#145626,#145627,#145628,#145629,#145630,#145631,
#145632,#145633,#145634,#145635,#145636,#145637,#145638,#145639,#145640,
#145641,#145642,#145643,#145644,#145645,#145646,#145647,#145648,#145649,
#145650,#145651,#145652,#145653,#145654,#145655,#145656,#145657,#145658,
#145659,#145660,#145661,#145662,#145663),.UNSPECIFIED.,.F.,.F.,(4,3,3,3,
3,3,3,3,3,3,3,3,3,3,3,3,3,3,3,3,3,3,3,3,3,3,3,3,3,3,3,3,3,3,3,3,3,3,3,3,
3,3,4),(53.4070751110266,53.5048543854907,53.6024983707772,53.7000367768846,
53.7975186210126,53.8949743677963,53.9924344477706,54.0899931990358,54.1876041339868,
54.2853815723763,54.3520848503674,54.4506829753711,54.5491407581477,54.6493633259204,
54.7476428836485,54.8458894627219,54.9441325457602,55.0458297344025,55.1442141478213,
55.2475677240753,55.3509213003293,55.4495194253331,55.5479772081099,55.6481997758826,
55.7464793336108,55.8447259126843,55.9429689957226,56.0446661843648,56.1430505977836,
56.2464041740374,56.3497577502912,56.4483558752949,56.5468136580715,56.6470362258442,
56.7453157835723,56.8435623626457,56.9418054456841,57.0435026343264,57.1418870477452,
57.2452406239991,57.3485942002531,57.4471969425955,57.4649113880947),
 .UNSPECIFIED.);
#1505=B_SPLINE_CURVE_WITH_KNOTS('',3,(#145669,#145670,#145671,#145672,#145673,
#145674,#145675,#145676),.UNSPECIFIED.,.F.,.F.,(4,1,1,1,1,4),(59.6902604182062,
59.8110738326964,60.8099102826583,61.8087467326202,62.807583182582,63.7472418219311),
 .UNSPECIFIED.);
#1506=B_SPLINE_CURVE_WITH_KNOTS('',3,(#145677,#145678,#145679,#145680,#145681,
#145682,#145683,#145684,#145685,#145686,#145687,#145688,#145689,#145690,
#145691,#145692,#145693,#145694,#145695,#145696,#145697,#145698,#145699,
#145700,#145701,#145702,#145703,#145704,#145705,#145706,#145707,#145708,
#145709,#145710,#145711,#145712,#145713,#145714,#145715,#145716,#145717,
#145718,#145719,#145720,#145721,#145722,#145723,#145724,#145725,#145726,
#145727,#145728,#145729,#145730,#145731,#145732,#145733,#145734,#145735,
#145736,#145737,#145738,#145739,#145740,#145741,#145742,#145743,#145744,
#145745,#145746),.UNSPECIFIED.,.F.,.F.,(4,3,3,3,3,3,3,3,3,3,3,3,3,3,3,3,
3,3,3,3,3,3,3,4),(57.4639959741701,57.5623571679093,57.6607771760175,57.759361977221,
57.8134009327727,57.9119990577764,58.0104568405532,58.1106794083258,58.208958966054,
58.3072055451274,58.4054486281659,58.507145816808,58.6055302302268,58.7088838064807,
58.8122373827345,58.9094791608007,59.0070768179764,59.1040671063403,59.2009981633324,
59.2979009849176,59.3959908432397,59.4929780422904,59.5916192302483,59.6902604182062),
 .UNSPECIFIED.);
#1507=B_SPLINE_CURVE_WITH_KNOTS('',3,(#145748,#145749,#145750,#145751,#145752,
#145753,#145754,#145755,#145756,#145757,#145758,#145759,#145760,#145761,
#145762,#145763,#145764,#145765,#145766,#145767,#145768,#145769,#145770,
#145771,#145772,#145773,#145774,#145775,#145776,#145777,#145778,#145779,
#145780,#145781,#145782,#145783,#145784,#145785,#145786,#145787,#145788,
#145789,#145790,#145791,#145792,#145793,#145794,#145795,#145796,#145797,
#145798,#145799,#145800,#145801,#145802,#145803,#145804,#145805,#145806,
#145807,#145808,#145809,#145810,#145811,#145812,#145813,#145814),
 .UNSPECIFIED.,.F.,.F.,(4,3,3,3,3,3,3,3,3,3,3,3,3,3,3,3,3,3,3,3,3,3,4),
(57.4649113880947,57.563347414557,57.6616774298067,57.7599496949233,57.858193723518,
57.9564389944101,58.0547832866313,58.1531751872017,58.2517448734333,58.3474306502149,
58.4460287752185,58.544486557995,58.6447091257677,58.7429886834959,58.8412352625694,
58.9394783456078,59.0411755342501,59.1395599476689,59.2429135239229,59.3462671001768,
59.4608829140295,59.5755716660044,59.6902604179793),.UNSPECIFIED.);
#1508=B_SPLINE_CURVE_WITH_KNOTS('',3,(#145815,#145816,#145817,#145818,#145819,
#145820,#145821,#145822,#145823,#145824,#145825,#145826,#145827,#145828,
#145829,#145830,#145831,#145832,#145833,#145834,#145835,#145836,#145837,
#145838,#145839,#145840,#145841,#145842,#145843,#145844,#145845,#145846,
#145847,#145848,#145849,#145850,#145851,#145852,#145853,#145854,#145855,
#145856,#145857,#145858,#145859,#145860,#145861,#145862,#145863,#145864,
#145865,#145866,#145867,#145868,#145869,#145870,#145871,#145872,#145873,
#145874,#145875,#145876,#145877,#145878,#145879,#145880,#145881,#145882,
#145883,#145884,#145885,#145886,#145887,#145888,#145889,#145890,#145891,
#145892,#145893,#145894,#145895,#145896,#145897,#145898,#145899,#145900,
#145901,#145902,#145903,#145904,#145905,#145906,#145907,#145908,#145909,
#145910,#145911,#145912,#145913,#145914,#145915,#145916,#145917,#145918,
#145919,#145920,#145921,#145922,#145923,#145924,#145925,#145926,#145927,
#145928,#145929,#145930,#145931,#145932,#145933,#145934,#145935,#145936,
#145937,#145938),.UNSPECIFIED.,.F.,.F.,(4,3,3,3,3,3,3,3,3,3,3,3,3,3,3,3,
3,3,3,3,3,3,3,3,3,3,3,3,3,3,3,3,3,3,3,3,3,3,3,3,3,4),(59.6902604182062,
59.788634173056,59.886998581597,59.9853827919993,60.0838846667643,60.1824499292137,
60.2811933482975,60.3451035501387,60.4437016751424,60.5421594579193,60.642382025692,
60.7406615834201,60.8389081624935,60.937151245532,61.0388484341742,61.1372328475929,
61.2405864238468,61.3439400001006,61.4425381251043,61.5409959078807,61.6412184756534,
61.7394980333816,61.8377446124549,61.9359876954935,62.0376848841357,62.1360692975546,
62.2394228738085,62.3427764500624,62.4413745750661,62.5398323578427,62.6400549256154,
62.7383344833436,62.836581062417,62.9348241454553,63.0365213340976,63.1349057475164,
63.2382593237703,63.3416129000243,63.4431811256632,63.5416227665057,63.6447542845429,
63.74788580258),.UNSPECIFIED.);
#1509=B_SPLINE_CURVE_WITH_KNOTS('',3,(#145944,#145945,#145946,#145947,#145948,
#145949,#145950,#145951,#145952,#145953,#145954,#145955,#145956,#145957,
#145958,#145959,#145960,#145961,#145962,#145963,#145964,#145965,#145966,
#145967,#145968,#145969,#145970,#145971,#145972,#145973,#145974,#145975,
#145976,#145977,#145978,#145979,#145980,#145981,#145982,#145983,#145984,
#145985,#145986,#145987,#145988,#145989,#145990,#145991,#145992,#145993,
#145994,#145995,#145996,#145997,#145998,#145999,#146000,#146001,#146002,
#146003,#146004,#146005,#146006,#146007,#146008,#146009,#146010,#146011,
#146012,#146013,#146014,#146015,#146016,#146017,#146018,#146019,#146020,
#146021,#146022,#146023,#146024,#146025,#146026,#146027,#146028,#146029,
#146030,#146031,#146032,#146033,#146034,#146035,#146036,#146037,#146038,
#146039,#146040,#146041,#146042,#146043,#146044,#146045,#146046,#146047,
#146048,#146049,#146050,#146051,#146052,#146053,#146054,#146055,#146056,
#146057,#146058,#146059,#146060,#146061,#146062,#146063,#146064,#146065,
#146066,#146067,#146068,#146069,#146070),.UNSPECIFIED.,.F.,.F.,(4,3,3,3,
3,3,3,3,3,3,3,3,3,3,3,3,3,3,3,3,3,3,3,3,3,3,3,3,3,3,3,3,3,3,3,3,3,3,3,3,
3,3,4),(65.9734457253857,66.0704340596178,66.1673127975358,66.264132888756,
66.360925426791,66.4577214670338,66.5546134226801,66.6515579893415,66.7486626585398,
66.8029289824295,66.9015271074332,66.9999848902101,67.1002074579827,67.1984870157109,
67.2967335947841,67.3949766778227,67.4966738664649,67.5950582798837,67.6984118561375,
67.8017654323914,67.9003635573952,67.998821340172,68.0990439079447,68.1973234656729,
68.2955700447463,68.3938131277848,68.4955103164269,68.5938947298458,68.6972483060995,
68.8006018823533,68.899200007357,68.9976577901336,69.0978803579063,69.1961599156345,
69.2944064947079,69.3926495777464,69.4943467663886,69.5927311798073,69.6960847560612,
69.7994383323151,69.8980412657737,69.9964918402282,70.0313849530686),
 .UNSPECIFIED.);
#1510=B_SPLINE_CURVE_WITH_KNOTS('',3,(#146071,#146072,#146073,#146074,#146075,
#146076,#146077),.UNSPECIFIED.,.F.,.F.,(4,1,1,1,4),(63.7472418219311,63.8064196325439,
64.8052560825058,65.8040925324676,65.9734457253857),.UNSPECIFIED.);
#1511=B_SPLINE_CURVE_WITH_KNOTS('',3,(#146079,#146080,#146081,#146082,#146083,
#146084,#146085,#146086,#146087,#146088,#146089,#146090,#146091,#146092,
#146093,#146094,#146095,#146096,#146097,#146098,#146099,#146100,#146101,
#146102,#146103,#146104,#146105,#146106,#146107,#146108,#146109,#146110,
#146111,#146112,#146113,#146114,#146115,#146116,#146117,#146118,#146119,
#146120,#146121,#146122,#146123,#146124,#146125,#146126,#146127,#146128,
#146129,#146130,#146131,#146132,#146133,#146134,#146135,#146136,#146137,
#146138,#146139,#146140,#146141,#146142,#146143,#146144,#146145,#146146,
#146147,#146148),.UNSPECIFIED.,.F.,.F.,(4,3,3,3,3,3,3,3,3,3,3,3,3,3,3,3,
3,3,3,3,3,3,3,4),(63.74788580258,63.8461305686218,63.9443750524778,64.0433936268549,
64.1417828266295,64.2411160883078,64.3404493499862,64.4390474749899,64.5375052577665,
64.6377278255392,64.7360073832674,64.8342539623407,64.932497045379,65.0341942340213,
65.1325786474401,65.2359322236941,65.3392857999481,65.4384637976085,65.53749807745,
65.6364173808604,65.7352455972606,65.8340208922139,65.932784900221,65.9734457253857),
 .UNSPECIFIED.);
#1512=B_SPLINE_CURVE_WITH_KNOTS('',3,(#146149,#146150,#146151,#146152,#146153,
#146154,#146155,#146156,#146157,#146158,#146159,#146160,#146161,#146162,
#146163,#146164,#146165,#146166,#146167,#146168,#146169,#146170,#146171,
#146172,#146173,#146174,#146175,#146176,#146177,#146178,#146179,#146180,
#146181,#146182,#146183,#146184,#146185,#146186,#146187,#146188,#146189,
#146190,#146191,#146192,#146193,#146194,#146195,#146196,#146197,#146198,
#146199,#146200,#146201,#146202,#146203,#146204,#146205,#146206,#146207,
#146208,#146209,#146210,#146211,#146212,#146213,#146214,#146215,#146216,
#146217,#146218,#146219,#146220,#146221,#146222,#146223,#146224,#146225,
#146226,#146227,#146228,#146229,#146230,#146231,#146232,#146233,#146234,
#146235,#146236,#146237,#146238,#146239,#146240,#146241,#146242,#146243,
#146244,#146245,#146246,#146247,#146248,#146249,#146250,#146251,#146252,
#146253,#146254,#146255,#146256,#146257,#146258,#146259,#146260,#146261,
#146262,#146263,#146264,#146265,#146266,#146267,#146268,#146269,#146270,
#146271,#146272),.UNSPECIFIED.,.F.,.F.,(4,3,3,3,3,3,3,3,3,3,3,3,3,3,3,3,
3,3,3,3,3,3,3,3,3,3,3,3,3,3,3,3,3,3,3,3,3,3,3,3,3,4),(65.9734457256204,
66.0848798050736,66.1968635637033,66.3094957826818,66.3381222499099,66.4367203749136,
66.5351781576903,66.635400725463,66.7336802831912,66.8319268622646,66.930169945303,
67.0318671339452,67.130251547364,67.2336051236179,67.3369586998718,67.4355568248755,
67.5340146076523,67.634237175425,67.7325167331532,67.8307633122265,67.9290063952651,
68.0307035839073,68.1290879973261,68.2324415735799,68.3357951498337,68.4343932748374,
68.5328510576141,68.6330736253868,68.7313531831149,68.8295997621883,68.9278428452268,
69.029540033869,69.1279244472878,69.2312780235417,69.3346315997956,69.433207943647,
69.5316540255013,69.6299995615608,69.7300684022547,69.8283147727187,69.9292948485276,
70.0302749243365),.UNSPECIFIED.);
#1513=B_SPLINE_CURVE_WITH_KNOTS('',3,(#146278,#146279,#146280,#146281,#146282,
#146283,#146284,#146285),.UNSPECIFIED.,.F.,.F.,(4,1,1,1,1,4),(72.2566310325654,
72.7959476822008,73.7947841321626,74.7936205821245,75.7924570320864,76.3138574567704),
 .UNSPECIFIED.);
#1514=B_SPLINE_CURVE_WITH_KNOTS('',3,(#146286,#146287,#146288,#146289,#146290,
#146291,#146292,#146293,#146294,#146295,#146296,#146297,#146298,#146299,
#146300,#146301,#146302,#146303,#146304,#146305,#146306,#146307,#146308,
#146309,#146310,#146311,#146312,#146313,#146314,#146315,#146316,#146317,
#146318,#146319,#146320,#146321,#146322,#146323,#146324,#146325,#146326,
#146327,#146328,#146329,#146330,#146331,#146332,#146333,#146334,#146335,
#146336,#146337,#146338,#146339,#146340,#146341,#146342,#146343,#146344,
#146345,#146346,#146347,#146348,#146349,#146350,#146351,#146352,#146353,
#146354,#146355),.UNSPECIFIED.,.F.,.F.,(4,3,3,3,3,3,3,3,3,3,3,3,3,3,3,3,
3,3,3,3,3,3,3,4),(70.0313849530686,70.1297027427429,70.2279679449009,70.3262100651504,
70.4244585789561,70.522809277639,70.6212122122823,70.7197874335469,70.798274782277,
70.8968729072806,70.9953306900573,71.09555325783,71.193832815558,71.2920793946316,
71.39032247767,71.4920196663122,71.590404079731,71.6937576559849,71.7971112322389,
71.902834090551,72.0081993817376,72.1133399321502,72.2181701837246,72.2566308185778),
 .UNSPECIFIED.);
#1515=B_SPLINE_CURVE_WITH_KNOTS('',3,(#146357,#146358,#146359,#146360,#146361,
#146362,#146363,#146364,#146365,#146366,#146367,#146368,#146369,#146370,
#146371,#146372,#146373,#146374,#146375,#146376,#146377,#146378,#146379,
#146380,#146381,#146382,#146383,#146384,#146385,#146386,#146387,#146388,
#146389,#146390,#146391,#146392,#146393,#146394,#146395,#146396,#146397,
#146398,#146399,#146400,#146401,#146402,#146403,#146404,#146405,#146406,
#146407,#146408,#146409,#146410,#146411,#146412,#146413,#146414,#146415,
#146416,#146417,#146418,#146419,#146420,#146421,#146422,#146423,#146424,
#146425,#146426),.UNSPECIFIED.,.F.,.F.,(4,3,3,3,3,3,3,3,3,3,3,3,3,3,3,3,
3,3,3,3,3,3,3,4),(70.0302749243365,70.1286604525724,70.2310642511649,70.3334680497574,
70.4320661747611,70.5305239575378,70.6307465253105,70.7290260830387,70.8272726621121,
70.9255157451506,71.0272129337928,71.1255973472116,71.2289509234654,71.3323044997193,
71.4298807240688,71.527317634942,71.6246428433669,71.7219081150619,71.8191441424516,
71.9163815796695,72.013708783522,72.1110862397604,72.208614546431,72.2566310325654),
 .UNSPECIFIED.);
#1516=B_SPLINE_CURVE_WITH_KNOTS('',3,(#146427,#146428,#146429,#146430,#146431,
#146432,#146433,#146434),.UNSPECIFIED.,.F.,.F.,(4,1,1,1,1,4),(72.2566310325654,
72.3311409496812,73.3299773996431,74.3288138496049,75.3276502995668,76.3138964141676),
 .UNSPECIFIED.);
#1517=B_SPLINE_CURVE_WITH_KNOTS('',3,(#146440,#146441,#146442,#146443,#146444,
#146445,#146446,#146447,#146448,#146449,#146450,#146451,#146452,#146453,
#146454,#146455,#146456,#146457,#146458,#146459,#146460,#146461,#146462,
#146463,#146464,#146465,#146466,#146467,#146468,#146469,#146470,#146471,
#146472,#146473,#146474,#146475,#146476,#146477,#146478,#146479,#146480,
#146481,#146482,#146483,#146484,#146485,#146486,#146487,#146488,#146489,
#146490,#146491,#146492,#146493,#146494,#146495,#146496,#146497,#146498,
#146499,#146500,#146501,#146502,#146503,#146504,#146505,#146506,#146507,
#146508,#146509,#146510,#146511,#146512,#146513,#146514,#146515,#146516,
#146517,#146518,#146519,#146520,#146521,#146522,#146523,#146524,#146525,
#146526,#146527,#146528,#146529,#146530,#146531,#146532,#146533,#146534,
#146535,#146536,#146537,#146538,#146539,#146540,#146541,#146542,#146543,
#146544,#146545,#146546,#146547,#146548,#146549,#146550,#146551,#146552,
#146553,#146554,#146555,#146556,#146557,#146558,#146559,#146560,#146561,
#146562,#146563),.UNSPECIFIED.,.F.,.F.,(4,3,3,3,3,3,3,3,3,3,3,3,3,3,3,3,
3,3,3,3,3,3,3,3,3,3,3,3,3,3,3,3,3,3,3,3,3,3,3,3,3,4),(78.5398164398193,
78.6677108218625,78.788966381972,78.8875645069757,78.9860222897523,79.086244857525,
79.1845244152531,79.2827709943265,79.3810140773651,79.4827112660073,79.5810956794261,
79.68444925568,79.7878028319339,79.8864009569376,79.9848587397144,80.085081307487,
80.1833608652152,80.2816074442886,80.379850527327,80.4815477159692,80.579932129388,
80.6832857056419,80.7866392818958,80.8852374068995,80.9836951896763,81.0839177574489,
81.1821973151771,81.2804438942505,81.378686977289,81.4803841659311,81.5787685793499,
81.6821221556038,81.7854757318576,81.8868624838438,81.9852993428627,82.0836395040165,
82.1819125660622,82.2801480557045,82.3784063416034,82.4766798080588,82.5750348031723,
82.5965697477472),.UNSPECIFIED.);
#1518=B_SPLINE_CURVE_WITH_KNOTS('',3,(#146564,#146565,#146566,#146567,#146568,
#146569),.UNSPECIFIED.,.F.,.F.,(4,1,1,4),(76.3138574567704,76.7912934820483,
77.7901299320101,78.539816339745),.UNSPECIFIED.);
#1519=B_SPLINE_CURVE_WITH_KNOTS('',3,(#146571,#146572,#146573,#146574,#146575,
#146576,#146577),.UNSPECIFIED.,.F.,.F.,(4,1,1,1,4),(76.3138964141676,76.3264867495287,
77.3253231994906,78.3241596494524,78.539816339745),.UNSPECIFIED.);
#1520=B_SPLINE_CURVE_WITH_KNOTS('',3,(#146578,#146579,#146580,#146581,#146582,
#146583,#146584,#146585,#146586,#146587,#146588,#146589,#146590,#146591,
#146592,#146593,#146594,#146595,#146596,#146597,#146598,#146599,#146600,
#146601,#146602,#146603,#146604,#146605,#146606,#146607,#146608,#146609,
#146610,#146611,#146612,#146613,#146614,#146615,#146616,#146617,#146618,
#146619,#146620,#146621,#146622,#146623,#146624,#146625,#146626,#146627,
#146628,#146629,#146630,#146631,#146632,#146633,#146634,#146635,#146636,
#146637,#146638,#146639,#146640,#146641,#146642,#146643,#146644,#146645,
#146646,#146647,#146648,#146649,#146650,#146651,#146652,#146653,#146654,
#146655,#146656,#146657,#146658,#146659,#146660,#146661,#146662,#146663,
#146664,#146665,#146666,#146667,#146668,#146669,#146670,#146671,#146672,
#146673,#146674,#146675,#146676,#146677,#146678,#146679,#146680,#146681,
#146682,#146683,#146684,#146685,#146686,#146687,#146688,#146689,#146690,
#146691,#146692,#146693,#146694,#146695,#146696,#146697,#146698,#146699,
#146700,#146701),.UNSPECIFIED.,.F.,.F.,(4,3,3,3,3,3,3,3,3,3,3,3,3,3,3,3,
3,3,3,3,3,3,3,3,3,3,3,3,3,3,3,3,3,3,3,3,3,3,3,3,3,4),(78.539816339745,78.6377138097037,
78.7346673304386,78.8315786913981,78.9284788661295,79.0271081744507,79.1241353185129,
79.2235657089636,79.3229960994143,79.421594224418,79.5200520071949,79.6202745749676,
79.7185541326958,79.8168007117692,79.9150437948077,80.0167409834498,80.1151253968686,
80.2184789731224,80.3218325493762,80.4204306743798,80.5188884571566,80.6191110249293,
80.7173905826574,80.8156371617309,80.9138802447695,81.0155774334116,81.1139618468305,
81.2173154230843,81.3206689993381,81.4192671243418,81.5177249071187,81.6179474748913,
81.7162270326194,81.8144736116928,81.9127166947312,82.0144138833734,82.1127982967921,
82.216151873046,82.3195054492999,82.4180964129948,82.5165362141343,82.5977152891205),
 .UNSPECIFIED.);
#1521=B_SPLINE_CURVE_WITH_KNOTS('',3,(#146707,#146708,#146709,#146710,#146711,
#146712,#146713,#146714),.UNSPECIFIED.,.F.,.F.,(4,1,1,1,1,4),(84.8230070319842,
85.7808215317051,86.779657981667,87.7784944316289,88.7773308815908,88.8809435690823),
 .UNSPECIFIED.);
#1522=B_SPLINE_CURVE_WITH_KNOTS('',3,(#146715,#146716,#146717,#146718,#146719,
#146720,#146721,#146722,#146723,#146724,#146725,#146726,#146727,#146728,
#146729,#146730,#146731,#146732,#146733,#146734,#146735,#146736,#146737,
#146738,#146739,#146740,#146741,#146742,#146743,#146744,#146745,#146746,
#146747,#146748,#146749,#146750,#146751,#146752,#146753,#146754,#146755,
#146756,#146757,#146758,#146759,#146760,#146761,#146762,#146763,#146764,
#146765,#146766,#146767,#146768,#146769,#146770,#146771,#146772,#146773,
#146774,#146775,#146776,#146777,#146778,#146779,#146780,#146781,#146782,
#146783,#146784),.UNSPECIFIED.,.F.,.F.,(4,3,3,3,3,3,3,3,3,3,3,3,3,3,3,3,
3,3,3,3,3,3,3,4),(82.5965697477472,82.6951414136759,82.7843121818195,82.8829103068232,
82.9813680895999,83.0815906573726,83.1798702151008,83.2781167941742,83.3763598772127,
83.4780570658548,83.5764414792737,83.6797950555275,83.7831486317814,83.8817467567851,
83.9802045395618,84.0804271073345,84.1787066650627,84.2769532441361,84.3751963271746,
84.4768935158168,84.5752779292356,84.6786315054894,84.7819850817433,84.8230016469246),
 .UNSPECIFIED.);
#1523=B_SPLINE_CURVE_WITH_KNOTS('',3,(#146786,#146787,#146788,#146789,#146790,
#146791,#146792,#146793,#146794,#146795,#146796,#146797,#146798,#146799,
#146800,#146801,#146802,#146803,#146804,#146805,#146806,#146807,#146808,
#146809,#146810,#146811,#146812,#146813,#146814,#146815,#146816,#146817,
#146818,#146819,#146820,#146821,#146822,#146823,#146824,#146825,#146826,
#146827,#146828,#146829,#146830,#146831,#146832,#146833,#146834,#146835,
#146836,#146837,#146838,#146839,#146840,#146841,#146842,#146843,#146844,
#146845,#146846,#146847,#146848,#146849,#146850,#146851,#146852,#146853,
#146854,#146855),.UNSPECIFIED.,.F.,.F.,(4,3,3,3,3,3,3,3,3,3,3,3,3,3,3,3,
3,3,3,3,3,3,3,4),(82.5977152891205,82.6960046600494,82.7942553301755,82.892496787616,
82.9907585028357,83.0891304591162,83.1875671116892,83.2861621786639,83.3183418992618,
83.4169400242656,83.5153978070425,83.6156203748151,83.7138999325432,83.8121465116165,
83.9103895946547,84.012086783297,84.1104711967157,84.2138247729697,84.3171783492237,
84.4205578302506,84.5236543867486,84.626583481318,84.7292989065995,84.8230016469246),
 .UNSPECIFIED.);
#1524=B_SPLINE_CURVE_WITH_KNOTS('',3,(#146856,#146857,#146858,#146859,#146860,
#146861,#146862,#146863,#146864,#146865,#146866,#146867,#146868,#146869,
#146870,#146871,#146872,#146873,#146874,#146875,#146876,#146877,#146878,
#146879,#146880,#146881,#146882,#146883,#146884,#146885,#146886,#146887,
#146888,#146889,#146890,#146891,#146892,#146893,#146894,#146895,#146896,
#146897,#146898,#146899,#146900,#146901,#146902,#146903,#146904,#146905,
#146906,#146907,#146908,#146909,#146910,#146911,#146912,#146913,#146914,
#146915,#146916,#146917,#146918,#146919,#146920,#146921,#146922,#146923,
#146924,#146925,#146926,#146927,#146928,#146929,#146930,#146931,#146932,
#146933,#146934,#146935,#146936,#146937,#146938,#146939,#146940,#146941,
#146942,#146943,#146944,#146945,#146946,#146947,#146948,#146949,#146950,
#146951,#146952,#146953,#146954,#146955,#146956,#146957,#146958,#146959,
#146960,#146961,#146962,#146963,#146964,#146965,#146966,#146967,#146968,
#146969,#146970,#146971,#146972,#146973,#146974,#146975,#146976,#146977,
#146978,#146979),.UNSPECIFIED.,.F.,.F.,(4,3,3,3,3,3,3,3,3,3,3,3,3,3,3,3,
3,3,3,3,3,3,3,3,3,3,3,3,3,3,3,3,3,3,3,3,3,3,3,3,3,4),(84.8230016472006,
84.9261861619504,85.0296647966981,85.1332945907092,85.2372126194224,85.3160147991856,
85.4146129241893,85.513070706966,85.6132932747387,85.7115728324668,85.8098194115402,
85.9080624945787,86.0097596832209,86.1081440966397,86.2114976728935,86.3148512491474,
86.4134493741511,86.5119071569279,86.6121297247006,86.7104092824287,86.8086558615021,
86.9068989445406,87.0085961331828,87.1069805466016,87.2103341228554,87.3136876991093,
87.412285824113,87.5107436068898,87.6109661746625,87.7092457323906,87.807492311464,
87.9057353945025,88.0074325831447,88.1058169965635,88.2091705728174,88.3125241490712,
88.4111137865017,88.5095698168558,88.6079122101848,88.7061871882861,88.8044419893967,
88.8801389646388),.UNSPECIFIED.);
#1525=B_SPLINE_CURVE_WITH_KNOTS('',3,(#146985,#146986,#146987,#146988,#146989,
#146990,#146991,#146992,#146993,#146994,#146995,#146996,#146997,#146998,
#146999,#147000,#147001,#147002,#147003,#147004,#147005,#147006,#147007,
#147008,#147009,#147010,#147011,#147012,#147013,#147014,#147015,#147016,
#147017,#147018,#147019,#147020,#147021,#147022,#147023,#147024,#147025,
#147026,#147027,#147028,#147029,#147030,#147031,#147032,#147033,#147034,
#147035,#147036,#147037,#147038,#147039,#147040,#147041,#147042,#147043,
#147044,#147045,#147046,#147047,#147048,#147049,#147050,#147051,#147052,
#147053,#147054,#147055,#147056,#147057,#147058,#147059,#147060,#147061,
#147062,#147063,#147064,#147065,#147066,#147067,#147068,#147069,#147070,
#147071,#147072,#147073,#147074,#147075,#147076,#147077,#147078,#147079,
#147080,#147081,#147082,#147083,#147084,#147085,#147086,#147087,#147088,
#147089,#147090,#147091,#147092,#147093,#147094,#147095,#147096,#147097,
#147098,#147099,#147100,#147101,#147102,#147103,#147104,#147105,#147106,
#147107,#147108),.UNSPECIFIED.,.F.,.F.,(4,3,3,3,3,3,3,3,3,3,3,3,3,3,3,3,
3,3,3,3,3,3,3,3,3,3,3,3,3,3,3,3,3,3,3,3,3,3,3,3,3,4),(91.1061869541041,
91.204341964477,91.3024795334307,91.4006291648839,91.4988897541856,91.5972075103077,
91.6957053368613,91.7738402314764,91.8724383564801,91.9708961392568,92.0711187070295,
92.1693982647576,92.2676448438311,92.3658879268694,92.4675851155116,92.5659695289304,
92.6693231051843,92.7726766814383,92.871274806442,92.9697325892187,93.0699551569914,
93.1682347147195,93.2664812937929,93.3647243768313,93.4664215654735,93.5648059788923,
93.6681595551462,93.7715131314001,93.8701112564038,93.9685690391807,94.0687916069534,
94.1670711646815,94.2653177437549,94.3635608267937,94.4652580154358,94.5636424288545,
94.6669960051083,94.770349581362,94.8689185475027,94.9673651079972,95.065708303045,
95.1638473516788),.UNSPECIFIED.);
#1526=B_SPLINE_CURVE_WITH_KNOTS('',3,(#147109,#147110,#147111,#147112,#147113,
#147114),.UNSPECIFIED.,.F.,.F.,(4,1,1,4),(88.8809435690823,89.7761673315526,
90.7750037815145,91.1061798190633),.UNSPECIFIED.);
#1527=B_SPLINE_CURVE_WITH_KNOTS('',3,(#147116,#147117,#147118,#147119,#147120,
#147121,#147122,#147123,#147124,#147125,#147126,#147127,#147128,#147129,
#147130,#147131,#147132,#147133,#147134,#147135,#147136,#147137,#147138,
#147139,#147140,#147141,#147142,#147143,#147144,#147145,#147146,#147147,
#147148,#147149,#147150,#147151,#147152,#147153,#147154,#147155,#147156,
#147157,#147158,#147159,#147160,#147161,#147162,#147163,#147164,#147165,
#147166,#147167,#147168,#147169,#147170,#147171,#147172,#147173,#147174,
#147175,#147176,#147177,#147178,#147179,#147180,#147181,#147182,#147183,
#147184,#147185,#147186,#147187,#147188),.UNSPECIFIED.,.F.,.F.,(4,3,3,3,
3,3,3,3,3,3,3,3,3,3,3,3,3,3,3,3,3,3,3,3,4),(88.8801389646388,88.9783988089623,
89.0767679915452,89.1752004205634,89.2737928081253,89.3113605990331,89.4099587240368,
89.5084165068136,89.6086390745863,89.7069186323145,89.8051652113879,89.9034082944264,
90.0051054830685,90.1034898964873,90.2068434727411,90.3101970489949,90.409695787095,
90.5067185530535,90.6036495481491,90.7005198981799,90.801936662084,90.8988156754797,
90.9957205549586,91.0927209416412,91.1061869537961),.UNSPECIFIED.);
#1528=B_SPLINE_CURVE_WITH_KNOTS('',3,(#147189,#147190,#147191,#147192,#147193,
#147194,#147195,#147196,#147197,#147198,#147199,#147200,#147201,#147202,
#147203,#147204,#147205,#147206,#147207,#147208,#147209,#147210,#147211,
#147212,#147213,#147214,#147215,#147216,#147217,#147218,#147219,#147220,
#147221,#147222,#147223,#147224,#147225,#147226,#147227,#147228,#147229,
#147230,#147231,#147232,#147233,#147234,#147235,#147236,#147237,#147238,
#147239,#147240,#147241,#147242,#147243,#147244,#147245,#147246,#147247,
#147248,#147249,#147250,#147251,#147252,#147253,#147254,#147255,#147256,
#147257,#147258,#147259,#147260,#147261,#147262,#147263,#147264,#147265,
#147266,#147267,#147268,#147269,#147270,#147271,#147272,#147273,#147274,
#147275,#147276,#147277,#147278,#147279,#147280,#147281,#147282,#147283,
#147284,#147285,#147286,#147287,#147288,#147289,#147290,#147291,#147292,
#147293,#147294,#147295,#147296,#147297,#147298,#147299,#147300,#147301,
#147302,#147303,#147304,#147305,#147306,#147307,#147308,#147309,#147310,
#147311,#147312),.UNSPECIFIED.,.F.,.F.,(4,3,3,3,3,3,3,3,3,3,3,3,3,3,3,3,
3,3,3,3,3,3,3,3,3,3,3,3,3,3,3,3,3,3,3,3,3,3,3,3,3,4),(91.1061869541041,
91.246503559673,91.3090334989568,91.4076316239605,91.5060894067373,91.6063119745099,
91.7045915322381,91.8028381113116,91.9010811943501,92.0027783829923,92.101162796411,
92.2045163726649,92.3078699489187,92.4064680739224,92.5049258566991,92.6051484244718,
92.7034279822,92.8016745612733,92.8999176443118,93.001614832954,93.0999992463728,
93.2033528226267,93.3067063988806,93.4053045238843,93.5037623066611,93.6039848744337,
93.7022644321619,93.8005110112352,93.8987540942737,94.0004512829159,94.0988356963347,
94.2021892725885,94.3055428488424,94.4041508037231,94.5025891903028,94.6009312472701,
94.6992065724882,94.7974446925385,94.8957159603378,94.9940021459977,95.0923959722068,
95.1629909686178),.UNSPECIFIED.);
#1529=B_SPLINE_CURVE_WITH_KNOTS('',3,(#147318,#147319,#147320,#147321,#147322,
#147323,#147324,#147325),.UNSPECIFIED.,.F.,.F.,(4,1,1,1,1,4),(97.3893797695142,
97.7668589312476,98.7656953812095,99.7645318311714,100.763368281133,101.445902003198),
 .UNSPECIFIED.);
#1530=B_SPLINE_CURVE_WITH_KNOTS('',3,(#147326,#147327,#147328,#147329,#147330,
#147331,#147332,#147333,#147334,#147335,#147336,#147337,#147338,#147339,
#147340,#147341,#147342,#147343,#147344,#147345,#147346,#147347,#147348,
#147349,#147350,#147351,#147352,#147353,#147354,#147355,#147356,#147357,
#147358,#147359,#147360,#147361,#147362,#147363,#147364,#147365,#147366,
#147367,#147368,#147369,#147370,#147371,#147372,#147373,#147374,#147375,
#147376,#147377,#147378,#147379,#147380,#147381,#147382,#147383,#147384,
#147385,#147386,#147387,#147388,#147389,#147390,#147391,#147392,#147393,
#147394,#147395,#147396,#147397,#147398),.UNSPECIFIED.,.F.,.F.,(4,3,3,3,
3,3,3,3,3,3,3,3,3,3,3,3,3,3,3,3,3,3,3,3,4),(95.1638473516788,95.2620943195394,
95.3603371734009,95.4625493878816,95.5609329012682,95.6593867584473,95.7579931908366,
95.7691860313239,95.8677841563275,95.9662419391037,96.0664645068765,96.1647440646045,
96.2629906436779,96.361233726716,96.4629309153584,96.5613153287773,96.6646689050316,
96.7680224812858,96.8674993725788,96.9668292609825,97.0660403563896,97.1651524247991,
97.2642075332237,97.3632407686266,97.3893722612837),.UNSPECIFIED.);
#1531=B_SPLINE_CURVE_WITH_KNOTS('',3,(#147400,#147401,#147402,#147403,#147404,
#147405,#147406,#147407,#147408,#147409,#147410,#147411,#147412,#147413,
#147414,#147415,#147416,#147417,#147418,#147419,#147420,#147421,#147422,
#147423,#147424,#147425,#147426,#147427,#147428,#147429,#147430,#147431,
#147432,#147433,#147434,#147435,#147436,#147437,#147438,#147439,#147440,
#147441,#147442,#147443,#147444,#147445,#147446,#147447,#147448,#147449,
#147450,#147451,#147452,#147453,#147454,#147455,#147456,#147457,#147458,
#147459,#147460,#147461,#147462,#147463,#147464,#147465,#147466,#147467,
#147468,#147469),.UNSPECIFIED.,.F.,.F.,(4,3,3,3,3,3,3,3,3,3,3,3,3,3,3,3,
3,3,3,3,3,3,3,4),(95.1629909686178,95.2615808482906,95.3043792988043,95.402977423808,
95.5014352065848,95.6016577743574,95.6999373320856,95.7981839111589,95.8964269941975,
95.9981241828397,96.0965085962585,96.1998621725123,96.3032157487662,96.4018138737699,
96.5002716565466,96.6004942243193,96.6987737820475,96.7970203611208,96.8952634441593,
96.9969606328015,97.0953450462203,97.1986986224741,97.302052198728,97.3893722612837),
 .UNSPECIFIED.);
#1532=B_SPLINE_CURVE_WITH_KNOTS('',3,(#147470,#147471,#147472,#147473,#147474,
#147475,#147476,#147477),.UNSPECIFIED.,.F.,.F.,(4,1,1,1,1,4),(97.3893809712563,
98.3008886486899,99.2997250986518,100.298561548614,101.297397998576,101.447496664675),
 .UNSPECIFIED.);
#1533=B_SPLINE_CURVE_WITH_KNOTS('',3,(#147483,#147484,#147485,#147486,#147487,
#147488,#147489,#147490,#147491,#147492,#147493,#147494,#147495,#147496,
#147497,#147498,#147499,#147500,#147501,#147502,#147503,#147504,#147505,
#147506,#147507,#147508,#147509,#147510,#147511,#147512,#147513,#147514,
#147515,#147516,#147517,#147518,#147519,#147520,#147521,#147522,#147523,
#147524,#147525,#147526,#147527,#147528,#147529,#147530,#147531,#147532,
#147533,#147534,#147535,#147536,#147537,#147538,#147539,#147540,#147541,
#147542,#147543,#147544,#147545,#147546,#147547,#147548,#147549,#147550,
#147551,#147552,#147553,#147554,#147555,#147556,#147557,#147558,#147559,
#147560,#147561,#147562,#147563,#147564,#147565,#147566,#147567,#147568,
#147569,#147570,#147571,#147572,#147573,#147574,#147575,#147576,#147577,
#147578,#147579,#147580,#147581,#147582,#147583,#147584,#147585,#147586,
#147587,#147588,#147589,#147590,#147591,#147592,#147593,#147594,#147595,
#147596,#147597,#147598,#147599,#147600,#147601,#147602,#147603,#147604,
#147605,#147606),.UNSPECIFIED.,.F.,.F.,(4,3,3,3,3,3,3,3,3,3,3,3,3,3,3,3,
3,3,3,3,3,3,3,3,3,3,3,3,3,3,3,3,3,3,3,3,3,3,3,3,3,4),(103.672557568463,
103.759877631019,103.858475756023,103.9569335388,104.057156106572,104.1554356643,
104.253682243374,104.351925326412,104.453622515054,104.552006928473,104.655360504727,
104.758714080981,104.857312205985,104.955769988762,105.055992556534,105.154272114262,
105.252518693336,105.350761776374,105.452458965017,105.550843378435,105.654196954689,
105.757550530943,105.856148655947,105.954606438723,106.054829006496,106.153108564224,
106.251355143298,106.349598226336,106.451295414978,106.549679828397,106.653033404651,
106.756386980905,106.854986798947,106.953445809627,107.05178876834,107.150068003063,
107.248313037023,107.346553353057,107.444881222508,107.543251670465,107.641785788185,
107.729756570279),.UNSPECIFIED.);
#1534=B_SPLINE_CURVE_WITH_KNOTS('',3,(#147607,#147608,#147609,#147610,#147611,
#147612),.UNSPECIFIED.,.F.,.F.,(4,1,1,4),(101.445902003198,101.762204731095,
102.761041181057,103.672548858943),.UNSPECIFIED.);
#1535=B_SPLINE_CURVE_WITH_KNOTS('',3,(#147614,#147615,#147616,#147617,#147618,
#147619),.UNSPECIFIED.,.F.,.F.,(4,1,1,4),(101.447496664675,102.296234448537,
103.295070898499,103.672550060648),.UNSPECIFIED.);
#1536=B_SPLINE_CURVE_WITH_KNOTS('',3,(#147620,#147621,#147622,#147623,#147624,
#147625,#147626,#147627,#147628,#147629,#147630,#147631,#147632,#147633,
#147634,#147635,#147636,#147637,#147638,#147639,#147640,#147641,#147642,
#147643,#147644,#147645,#147646,#147647,#147648,#147649,#147650,#147651,
#147652,#147653,#147654,#147655,#147656,#147657,#147658,#147659,#147660,
#147661,#147662,#147663,#147664,#147665,#147666,#147667,#147668,#147669,
#147670,#147671,#147672,#147673,#147674,#147675,#147676,#147677,#147678,
#147679,#147680,#147681,#147682,#147683,#147684,#147685,#147686,#147687,
#147688,#147689,#147690,#147691,#147692,#147693,#147694,#147695,#147696,
#147697,#147698,#147699,#147700,#147701,#147702,#147703,#147704,#147705,
#147706,#147707,#147708,#147709,#147710,#147711,#147712,#147713,#147714,
#147715,#147716,#147717,#147718,#147719,#147720,#147721,#147722,#147723,
#147724,#147725,#147726,#147727,#147728,#147729,#147730,#147731,#147732,
#147733,#147734,#147735,#147736,#147737,#147738,#147739,#147740,#147741,
#147742,#147743,#147744,#147745,#147746),.UNSPECIFIED.,.F.,.F.,(4,3,3,3,
3,3,3,3,3,3,3,3,3,3,3,3,3,3,3,3,3,3,3,3,3,3,3,3,3,3,3,3,3,3,3,3,3,3,3,3,
3,3,4),(103.672557568463,103.771601702603,103.870660322484,103.96976131202,
104.06899945985,104.168318657834,104.267812431338,104.293907348461,104.392505473465,
104.490963256242,104.591185824014,104.689465381742,104.787711960816,104.885955043854,
104.987652232497,105.086036645915,105.189390222169,105.292743798423,105.391341923427,
105.489799706203,105.590022273976,105.688301831704,105.786548410778,105.884791493816,
105.986488682458,106.084873095877,106.188226672131,106.291580248385,106.390178373389,
106.488636156165,106.588858723938,106.687138281666,106.78538486074,106.883627943778,
106.98532513242,107.083709545839,107.187063122093,107.290416698347,107.389023062569,
107.487464394918,107.585810440421,107.684086111431,107.730086441502),
 .UNSPECIFIED.);
#1537=B_SPLINE_CURVE_WITH_KNOTS('',3,(#147752,#147753,#147754,#147755,#147756,
#147757,#147758,#147759,#147760,#147761,#147762,#147763,#147764,#147765,
#147766,#147767,#147768,#147769,#147770,#147771,#147772,#147773,#147774,
#147775,#147776,#147777,#147778,#147779,#147780,#147781,#147782,#147783,
#147784,#147785,#147786,#147787,#147788,#147789,#147790,#147791,#147792,
#147793,#147794,#147795,#147796,#147797,#147798,#147799,#147800,#147801,
#147802,#147803,#147804,#147805,#147806,#147807,#147808,#147809,#147810,
#147811,#147812,#147813,#147814,#147815,#147816,#147817,#147818,#147819,
#147820,#147821,#147822,#147823,#147824,#147825,#147826,#147827,#147828,
#147829,#147830,#147831,#147832,#147833,#147834,#147835,#147836,#147837,
#147838,#147839,#147840,#147841,#147842,#147843,#147844,#147845,#147846,
#147847,#147848,#147849,#147850,#147851,#147852,#147853,#147854,#147855,
#147856,#147857,#147858,#147859,#147860,#147861,#147862,#147863,#147864,
#147865,#147866,#147867,#147868,#147869,#147870,#147871,#147872,#147873,
#147874,#147875,#147876,#147877,#147878),.UNSPECIFIED.,.F.,.F.,(4,3,3,3,
3,3,3,3,3,3,3,3,3,3,3,3,3,3,3,3,3,3,3,3,3,3,3,3,3,3,3,3,3,3,3,3,3,3,3,3,
3,3,4),(109.955742875951,110.055241614051,110.152151423466,110.249014842069,
110.345862894414,110.447330365999,110.544300028994,110.641334438529,110.738518045248,
110.751732780752,110.850330905756,110.948788688533,111.049011256305,111.147290814033,
111.245537393107,111.343780476145,111.445477664787,111.543862078206,111.64721565446,
111.750569230714,111.849167355718,111.947625138494,112.047847706267,112.146127263995,
112.244373843069,112.342616926107,112.44431411475,112.542698528168,112.646052104422,
112.749405680676,112.84800380568,112.946461588456,113.046684156229,113.144963713957,
113.243210293031,113.341453376069,113.443150564711,113.54153497813,113.644888554384,
113.748242130638,113.846836224881,113.945278284699,114.013656826298),
 .UNSPECIFIED.);
#1538=B_SPLINE_CURVE_WITH_KNOTS('',3,(#147879,#147880,#147881,#147882,#147883,
#147884,#147885,#147886,#147887,#147888,#147889,#147890,#147891,#147892,
#147893,#147894,#147895,#147896,#147897,#147898,#147899,#147900,#147901,
#147902,#147903,#147904,#147905,#147906,#147907,#147908,#147909,#147910,
#147911,#147912,#147913,#147914,#147915,#147916,#147917,#147918,#147919,
#147920,#147921,#147922,#147923,#147924,#147925,#147926,#147927,#147928,
#147929,#147930,#147931,#147932,#147933,#147934,#147935,#147936,#147937,
#147938,#147939,#147940,#147941,#147942,#147943,#147944,#147945,#147946,
#147947,#147948),.UNSPECIFIED.,.F.,.F.,(4,3,3,3,3,3,3,3,3,3,3,3,3,3,3,3,
3,3,3,3,3,3,3,4),(107.729756570279,107.755223430866,107.85382155587,107.952279338646,
108.052501906419,108.150781464147,108.24902804322,108.347271126259,108.448968314901,
108.54735272832,108.650706304574,108.754059880828,108.852658005832,108.951115788608,
109.051338356381,109.149617914109,109.247864493183,109.346107576221,109.447804764863,
109.546189178282,109.649542754536,109.75289633079,109.893212936346,109.955742875643),
 .UNSPECIFIED.);
#1539=B_SPLINE_CURVE_WITH_KNOTS('',3,(#147950,#147951,#147952,#147953,#147954,
#147955,#147956,#147957,#147958,#147959,#147960,#147961,#147962,#147963,
#147964,#147965,#147966,#147967,#147968,#147969,#147970,#147971,#147972,
#147973,#147974,#147975,#147976,#147977,#147978,#147979,#147980,#147981,
#147982,#147983,#147984,#147985,#147986,#147987,#147988,#147989,#147990,
#147991,#147992,#147993,#147994,#147995,#147996,#147997,#147998,#147999,
#148000,#148001,#148002,#148003,#148004,#148005,#148006,#148007,#148008,
#148009,#148010,#148011,#148012,#148013,#148014,#148015,#148016,#148017,
#148018,#148019),.UNSPECIFIED.,.F.,.F.,(4,3,3,3,3,3,3,3,3,3,3,3,3,3,3,3,
3,3,3,3,3,3,3,4),(107.730086441502,107.828327805401,107.926578904311,108.024934190854,
108.123344715731,108.221924060079,108.289253148309,108.387851273313,108.486309056089,
108.586531623862,108.68481118159,108.783057760664,108.881300843702,108.982998032344,
109.081382445763,109.184736022017,109.288089598271,109.386591328535,109.484956309732,
109.583214317041,109.681399820023,109.779540599733,109.877698313764,109.955742875643),
 .UNSPECIFIED.);
#1540=B_SPLINE_CURVE_WITH_KNOTS('',3,(#148020,#148021,#148022,#148023,#148024,
#148025,#148026,#148027),.UNSPECIFIED.,.F.,.F.,(4,1,1,1,1,4),(109.955750010146,
110.286926048232,111.285762498194,112.284598948156,113.283435398118,114.01218696335),
 .UNSPECIFIED.);
#1541=B_SPLINE_CURVE_WITH_KNOTS('',3,(#148033,#148034,#148035,#148036,#148037,
#148038,#148039,#148040,#148041,#148042,#148043,#148044,#148045,#148046,
#148047,#148048,#148049,#148050,#148051,#148052,#148053,#148054,#148055,
#148056,#148057,#148058,#148059,#148060,#148061,#148062,#148063,#148064,
#148065,#148066,#148067,#148068,#148069,#148070,#148071,#148072,#148073,
#148074,#148075,#148076,#148077,#148078,#148079,#148080,#148081,#148082,
#148083,#148084,#148085,#148086,#148087,#148088,#148089,#148090,#148091,
#148092,#148093,#148094,#148095,#148096,#148097,#148098,#148099,#148100,
#148101,#148102,#148103,#148104,#148105,#148106,#148107,#148108,#148109,
#148110,#148111,#148112,#148113,#148114,#148115,#148116,#148117,#148118,
#148119,#148120,#148121,#148122,#148123,#148124,#148125,#148126,#148127,
#148128,#148129,#148130,#148131,#148132,#148133,#148134,#148135,#148136,
#148137,#148138,#148139,#148140,#148141,#148142,#148143,#148144,#148145,
#148146,#148147,#148148,#148149,#148150,#148151,#148152,#148153,#148154,
#148155,#148156),.UNSPECIFIED.,.F.,.F.,(4,3,3,3,3,3,3,3,3,3,3,3,3,3,3,3,
3,3,3,3,3,3,3,3,3,3,3,3,3,3,3,3,3,3,3,3,3,3,3,3,3,4),(116.238928182823,
116.341566510357,116.44447107289,116.547509821617,116.650828963887,116.744751480523,
116.843349605527,116.941807388303,117.042029956076,117.140309513804,117.238556092877,
117.336799175916,117.438496364558,117.536880777977,117.640234354231,117.743587930485,
117.842186055489,117.940643838265,118.040866406038,118.139145963766,118.23739254284,
118.335635625878,118.437332814521,118.535717227939,118.639070804193,118.742424380447,
118.841022505451,118.939480288228,119.039702856,119.137982413728,119.236228992802,
119.33447207584,119.436169264482,119.534553677901,119.637907254155,119.741260830409,
119.839851983056,119.938309194702,120.036651331111,120.134925920019,120.233176074199,
120.296103415561),.UNSPECIFIED.);
#1542=B_SPLINE_CURVE_WITH_KNOTS('',3,(#148157,#148158,#148159,#148160,#148161,
#148162,#148163,#148164,#148165,#148166,#148167,#148168,#148169,#148170,
#148171,#148172,#148173,#148174,#148175,#148176,#148177,#148178,#148179,
#148180,#148181,#148182,#148183,#148184,#148185,#148186,#148187,#148188,
#148189,#148190,#148191,#148192,#148193,#148194,#148195,#148196,#148197,
#148198,#148199,#148200,#148201,#148202,#148203,#148204,#148205,#148206,
#148207,#148208,#148209,#148210,#148211,#148212,#148213,#148214,#148215,
#148216,#148217,#148218,#148219,#148220,#148221,#148222,#148223,#148224,
#148225,#148226),.UNSPECIFIED.,.F.,.F.,(4,3,3,3,3,3,3,3,3,3,3,3,3,3,3,3,
3,3,3,3,3,3,3,4),(114.013656826298,114.111953403897,114.210207440612,114.308448428809,
114.406705839748,114.505071330138,114.60349806933,114.702086924788,114.747078580599,
114.845676705603,114.944134488379,115.044357056152,115.14263661388,115.240883192953,
115.339126275991,115.440823464634,115.539207878053,115.642561454307,115.745915030561,
115.849888759331,115.953561696348,116.057054365164,116.160309146371,116.238928182547),
 .UNSPECIFIED.);
#1543=B_SPLINE_CURVE_WITH_KNOTS('',3,(#148228,#148229,#148230,#148231,#148232,
#148233),.UNSPECIFIED.,.F.,.F.,(4,1,1,4),(114.01218696335,114.28227184808,
115.281108298042,116.238922797526),.UNSPECIFIED.);
#1544=B_SPLINE_CURVE_WITH_KNOTS('',3,(#148234,#148235,#148236,#148237,#148238,
#148239,#148240,#148241,#148242,#148243,#148244,#148245,#148246,#148247,
#148248,#148249,#148250,#148251,#148252,#148253,#148254,#148255,#148256,
#148257,#148258,#148259,#148260,#148261,#148262,#148263,#148264,#148265,
#148266,#148267,#148268,#148269,#148270,#148271,#148272,#148273,#148274,
#148275,#148276,#148277,#148278,#148279,#148280,#148281,#148282,#148283,
#148284,#148285,#148286,#148287,#148288,#148289,#148290,#148291,#148292,
#148293,#148294,#148295,#148296,#148297,#148298,#148299,#148300,#148301,
#148302,#148303,#148304,#148305,#148306,#148307,#148308,#148309,#148310,
#148311,#148312,#148313,#148314,#148315,#148316,#148317,#148318,#148319,
#148320,#148321,#148322,#148323,#148324,#148325,#148326,#148327,#148328,
#148329,#148330,#148331,#148332,#148333,#148334,#148335,#148336,#148337,
#148338,#148339,#148340,#148341,#148342,#148343,#148344,#148345,#148346,
#148347,#148348,#148349,#148350,#148351,#148352,#148353,#148354,#148355,
#148356,#148357,#148358,#148359,#148360),.UNSPECIFIED.,.F.,.F.,(4,3,3,3,
3,3,3,3,3,3,3,3,3,3,3,3,3,3,3,3,3,3,3,3,3,3,3,3,3,3,3,3,3,3,3,3,3,3,3,3,
3,3,4),(116.238928182823,116.279944748004,116.378542873008,116.477000655784,
116.577223223557,116.675502781285,116.773749360358,116.871992443397,116.973689632039,
117.072074045458,117.175427621712,117.278781197966,117.37737932297,117.475837105746,
117.576059673519,117.674339231247,117.77258581032,117.870828893359,117.972526082001,
118.07091049542,118.174264071673,118.277617647927,118.376215772931,118.474673555707,
118.57489612348,118.673175681208,118.771422260281,118.86966534332,118.971362531962,
119.069746945381,119.173100521635,119.276454097889,119.375052222893,119.47351000567,
119.573732573442,119.67201213117,119.770258710244,119.868501793282,119.970198981925,
120.068583395343,120.171936971597,120.275290547851,120.296396934293),
 .UNSPECIFIED.);
#1545=B_SPLINE_CURVE_WITH_KNOTS('',3,(#148366,#148367,#148368,#148369,#148370,
#148371,#148372,#148373),.UNSPECIFIED.,.F.,.F.,(4,1,1,1,1,4),(122.522113490002,
122.737770180294,123.736606630256,124.735443080218,125.73427953018,126.57866683563),
 .UNSPECIFIED.);
#1546=B_SPLINE_CURVE_WITH_KNOTS('',3,(#148374,#148375,#148376,#148377,#148378,
#148379,#148380,#148381,#148382,#148383,#148384,#148385,#148386,#148387,
#148388,#148389,#148390,#148391,#148392,#148393,#148394,#148395,#148396,
#148397,#148398,#148399,#148400,#148401,#148402,#148403,#148404,#148405,
#148406,#148407,#148408,#148409,#148410,#148411,#148412,#148413,#148414,
#148415,#148416,#148417,#148418,#148419,#148420,#148421,#148422,#148423,
#148424,#148425,#148426,#148427,#148428,#148429,#148430,#148431,#148432,
#148433,#148434,#148435,#148436,#148437,#148438,#148439,#148440,#148441,
#148442,#148443),.UNSPECIFIED.,.F.,.F.,(4,3,3,3,3,3,3,3,3,3,3,3,3,3,3,3,
3,3,3,3,3,3,3,4),(120.296103415561,120.394359169329,120.492722080471,120.59114479427,
120.689731208205,120.740097280371,120.838695405375,120.937153188151,121.037375755924,
121.135655313652,121.233901892726,121.332144975764,121.433842164406,121.532226577825,
121.635580154079,121.738933730333,121.836831200292,121.933909156543,122.030894120917,
122.127817176647,122.226391254986,122.323316910845,122.422715200424,122.522113490002),
 .UNSPECIFIED.);
#1547=B_SPLINE_CURVE_WITH_KNOTS('',3,(#148445,#148446,#148447,#148448,#148449,
#148450,#148451,#148452,#148453,#148454,#148455,#148456,#148457,#148458,
#148459,#148460,#148461,#148462,#148463,#148464,#148465,#148466,#148467,
#148468,#148469,#148470,#148471,#148472,#148473,#148474,#148475,#148476,
#148477,#148478,#148479,#148480,#148481,#148482,#148483,#148484,#148485,
#148486,#148487,#148488,#148489,#148490,#148491,#148492,#148493,#148494,
#148495,#148496,#148497,#148498,#148499,#148500,#148501,#148502,#148503,
#148504,#148505,#148506,#148507,#148508,#148509,#148510,#148511),
 .UNSPECIFIED.,.F.,.F.,(4,3,3,3,3,3,3,3,3,3,3,3,3,3,3,3,3,3,3,3,3,3,4),
(120.296396934293,120.394962268417,120.493394294901,120.59172185699,120.689992675083,
120.788236261167,120.886482093345,120.984827570553,121.083221557777,121.181792244442,
121.274126997813,121.372725122817,121.471182905593,121.571405473366,121.669685031094,
121.767931610168,121.866174693206,121.967871881848,122.066256295267,122.169609871521,
122.272963447775,122.400857829821,122.52211338997),.UNSPECIFIED.);
#1548=B_SPLINE_CURVE_WITH_KNOTS('',3,(#148512,#148513,#148514,#148515,#148516,
#148517,#148518,#148519),.UNSPECIFIED.,.F.,.F.,(4,1,1,1,1,4),(122.522113490002,
123.271799897737,124.270636347699,125.269472797661,126.268309247622,126.58028576884),
 .UNSPECIFIED.);
#1549=B_SPLINE_CURVE_WITH_KNOTS('',3,(#148525,#148526,#148527,#148528,#148529,
#148530,#148531,#148532,#148533,#148534,#148535,#148536,#148537,#148538,
#148539,#148540,#148541,#148542,#148543,#148544,#148545,#148546,#148547,
#148548,#148549,#148550,#148551,#148552,#148553,#148554,#148555,#148556,
#148557,#148558,#148559,#148560,#148561,#148562,#148563,#148564,#148565,
#148566,#148567,#148568,#148569,#148570,#148571,#148572,#148573,#148574,
#148575,#148576,#148577,#148578,#148579,#148580,#148581,#148582,#148583,
#148584,#148585,#148586,#148587,#148588,#148589,#148590,#148591,#148592,
#148593,#148594,#148595,#148596,#148597,#148598,#148599,#148600,#148601,
#148602,#148603,#148604,#148605,#148606,#148607,#148608,#148609,#148610,
#148611,#148612,#148613,#148614,#148615,#148616,#148617,#148618,#148619,
#148620,#148621,#148622,#148623,#148624,#148625,#148626,#148627,#148628,
#148629,#148630,#148631,#148632,#148633,#148634,#148635,#148636,#148637,
#148638,#148639,#148640,#148641,#148642,#148643,#148644,#148645,#148646,
#148647,#148648,#148649,#148650,#148651),.UNSPECIFIED.,.F.,.F.,(4,3,3,3,
3,3,3,3,3,3,3,3,3,3,3,3,3,3,3,3,3,3,3,3,3,3,3,3,3,3,3,3,3,3,3,3,3,3,3,3,
3,3,4),(128.805298797182,128.902840431273,129.000250613517,129.097560812666,
129.194818343698,129.292053887497,129.389298094495,129.486642967568,129.584044330746,
129.68160592498,129.729625330028,129.828223455032,129.926681237808,130.026903805581,
130.125183363309,130.223429942382,130.321673025421,130.423370214063,130.521754627482,
130.625108203735,130.728461779989,130.827059904993,130.92551768777,131.025740255542,
131.12401981327,131.222266392344,131.320509475382,131.422206664024,131.520591077443,
131.623944653697,131.727298229951,131.825896354955,131.924354137731,132.024576705504,
132.122856263232,132.221102842306,132.319345925344,132.421043113987,132.519427527405,
132.622781103659,132.726134679913,132.8247266372,132.863178388799),
 .UNSPECIFIED.);
#1550=B_SPLINE_CURVE_WITH_KNOTS('',3,(#148652,#148653,#148654,#148655,#148656,
#148657,#148658),.UNSPECIFIED.,.F.,.F.,(4,1,1,1,4),(126.57866683563,126.733115980142,
127.731952430104,128.730788880066,128.805298797182),.UNSPECIFIED.);
#1551=B_SPLINE_CURVE_WITH_KNOTS('',3,(#148660,#148661,#148662,#148663,#148664,
#148665),.UNSPECIFIED.,.F.,.F.,(4,1,1,4),(126.58028576884,127.267145697584,
128.265982147546,128.805298797182),.UNSPECIFIED.);
#1552=B_SPLINE_CURVE_WITH_KNOTS('',3,(#148666,#148667,#148668,#148669,#148670,
#148671,#148672,#148673,#148674,#148675,#148676,#148677,#148678,#148679,
#148680,#148681,#148682,#148683,#148684,#148685,#148686,#148687,#148688,
#148689,#148690,#148691,#148692,#148693,#148694,#148695,#148696,#148697,
#148698,#148699,#148700,#148701,#148702,#148703,#148704,#148705,#148706,
#148707,#148708,#148709,#148710,#148711,#148712,#148713,#148714,#148715,
#148716,#148717,#148718,#148719,#148720,#148721,#148722,#148723,#148724,
#148725,#148726,#148727,#148728,#148729,#148730,#148731,#148732,#148733,
#148734,#148735,#148736,#148737,#148738,#148739,#148740,#148741,#148742,
#148743,#148744,#148745,#148746,#148747,#148748,#148749,#148750,#148751,
#148752,#148753,#148754,#148755,#148756,#148757,#148758,#148759,#148760,
#148761,#148762,#148763,#148764,#148765,#148766,#148767,#148768,#148769,
#148770,#148771,#148772,#148773,#148774,#148775,#148776,#148777,#148778,
#148779,#148780,#148781,#148782,#148783,#148784,#148785,#148786,#148787,
#148788,#148789),.UNSPECIFIED.,.F.,.F.,(4,3,3,3,3,3,3,3,3,3,3,3,3,3,3,3,
3,3,3,3,3,3,3,3,3,3,3,3,3,3,3,3,3,3,3,3,3,3,3,3,3,4),(128.80529901116,128.910085619871,
129.015255759151,129.120630109632,129.226318351047,129.264818597508,129.363416722512,
129.461874505288,129.562097073061,129.660376630789,129.758623209863,129.856866292901,
129.958563481543,130.056947894962,130.160301471216,130.26365504747,130.362253172474,
130.46071095525,130.560933523023,130.659213080751,130.757459659825,130.855702742863,
130.957399931505,131.055784344924,131.159137921178,131.262491497432,131.361089622436,
131.459547405213,131.559769972985,131.658049530713,131.756296109787,131.854539192825,
131.956236381468,132.054620794886,132.15797437114,132.261327947394,132.359913784698,
132.458366887933,132.559360491667,132.657635694893,132.75998849888,132.862341302868),
 .UNSPECIFIED.);
#1553=B_SPLINE_CURVE_WITH_KNOTS('',3,(#148795,#148796,#148797,#148798,#148799,
#148800,#148801,#148802,#148803,#148804,#148805,#148806,#148807,#148808,
#148809,#148810,#148811,#148812,#148813,#148814,#148815,#148816,#148817,
#148818,#148819,#148820,#148821,#148822,#148823,#148824,#148825,#148826,
#148827,#148828,#148829,#148830,#148831,#148832,#148833,#148834,#148835,
#148836,#148837,#148838,#148839,#148840,#148841,#148842,#148843,#148844,
#148845,#148846,#148847,#148848,#148849,#148850,#148851,#148852,#148853,
#148854,#148855,#148856,#148857,#148858,#148859,#148860,#148861,#148862,
#148863,#148864,#148865,#148866,#148867,#148868,#148869,#148870,#148871,
#148872,#148873,#148874,#148875,#148876,#148877,#148878,#148879,#148880,
#148881,#148882,#148883,#148884,#148885,#148886,#148887,#148888,#148889,
#148890,#148891,#148892,#148893,#148894,#148895,#148896,#148897,#148898,
#148899,#148900,#148901,#148902,#148903,#148904,#148905,#148906,#148907,
#148908,#148909,#148910,#148911,#148912,#148913,#148914,#148915,#148916,
#148917,#148918,#148919,#148920,#148921),.UNSPECIFIED.,.F.,.F.,(4,3,3,3,
3,3,3,3,3,3,3,3,3,3,3,3,3,3,3,3,3,3,3,3,3,3,3,3,3,3,3,3,3,3,3,3,3,3,3,3,
3,3,4),(135.088484104361,135.187254556185,135.286029876603,135.384838499173,
135.483776463585,135.582788468008,135.681976179006,135.722644029799,135.821242154803,
135.919699937579,136.019922505352,136.11820206308,136.216448642154,136.314691725192,
136.416388913834,136.514773327253,136.618126903507,136.721480479761,136.820078604765,
136.918536387541,137.018758955314,137.117038513042,137.215285092115,137.313528175154,
137.415225363796,137.513609777215,137.616963353469,137.720316929723,137.818915054727,
137.917372837503,138.017595405276,138.115874963004,138.214121542077,138.312364625116,
138.414061813758,138.512446227177,138.61579980343,138.719153379684,138.817761602492,
138.916204188038,139.014551352302,139.112826031212,139.14605062869),
 .UNSPECIFIED.);
#1554=B_SPLINE_CURVE_WITH_KNOTS('',3,(#148922,#148923,#148924,#148925,#148926,
#148927,#148928,#148929,#148930,#148931,#148932,#148933,#148934,#148935,
#148936,#148937,#148938,#148939,#148940,#148941,#148942,#148943,#148944,
#148945,#148946,#148947,#148948,#148949,#148950,#148951,#148952,#148953,
#148954,#148955,#148956,#148957,#148958,#148959,#148960,#148961,#148962,
#148963,#148964,#148965,#148966,#148967,#148968,#148969,#148970,#148971,
#148972,#148973,#148974,#148975,#148976,#148977,#148978,#148979,#148980,
#148981,#148982,#148983,#148984,#148985,#148986,#148987,#148988,#148989,
#148990,#148991),.UNSPECIFIED.,.F.,.F.,(4,3,3,3,3,3,3,3,3,3,3,3,3,3,3,3,
3,3,3,3,3,3,3,4),(132.863178388799,132.961590306302,133.059905711635,133.158169582967,
133.256411424373,133.354660710732,133.453012816327,133.551418102536,133.649994575943,
133.724971129875,133.823569254879,133.922027037656,134.022249605428,134.120529163156,
134.21877574223,134.317018825268,134.41871601391,134.517100427329,134.620454003583,
134.723807579837,134.8363385207,134.948409000641,135.059693750753,135.088484104126),
 .UNSPECIFIED.);
#1555=B_SPLINE_CURVE_WITH_KNOTS('',3,(#148993,#148994,#148995,#148996,#148997,
#148998,#148999,#149000,#149001,#149002,#149003,#149004,#149005,#149006,
#149007,#149008,#149009,#149010,#149011,#149012,#149013,#149014,#149015,
#149016,#149017,#149018,#149019,#149020,#149021,#149022,#149023,#149024,
#149025,#149026,#149027,#149028,#149029,#149030,#149031,#149032,#149033,
#149034,#149035,#149036,#149037,#149038,#149039,#149040,#149041,#149042,
#149043,#149044,#149045,#149046,#149047,#149048,#149049,#149050,#149051,
#149052,#149053,#149054,#149055,#149056,#149057,#149058,#149059,#149060,
#149061,#149062),.UNSPECIFIED.,.F.,.F.,(4,3,3,3,3,3,3,3,3,3,3,3,3,3,3,3,
3,3,3,3,3,3,3,4),(132.862341302868,132.96179707649,133.060185482975,133.160174940165,
133.260164397356,133.35876252236,133.457220305136,133.557442872909,133.655722430637,
133.75396900971,133.852212092749,133.953909281391,134.05229369481,134.155647271063,
134.259000847317,134.356128675186,134.453094160804,134.549968416922,134.646782617699,
134.743567858737,134.840399971759,134.937256811785,135.034231214224,135.088484104361),
 .UNSPECIFIED.);
#1556=B_SPLINE_CURVE_WITH_KNOTS('',3,(#149063,#149064,#149065,#149066,#149067,
#149068,#149069,#149070),.UNSPECIFIED.,.F.,.F.,(4,1,1,1,1,4),(135.088484104361,
135.257837297279,136.256673747241,137.255510197203,138.254346647165,139.145213405918),
 .UNSPECIFIED.);
#1557=B_SPLINE_CURVE_WITH_KNOTS('',3,(#149076,#149077,#149078,#149079,#149080,
#149081,#149082,#149083,#149084,#149085,#149086,#149087,#149088,#149089,
#149090,#149091,#149092,#149093,#149094,#149095,#149096,#149097,#149098,
#149099,#149100,#149101,#149102,#149103,#149104,#149105,#149106,#149107,
#149108,#149109,#149110,#149111,#149112,#149113,#149114,#149115,#149116,
#149117,#149118,#149119,#149120,#149121,#149122,#149123,#149124,#149125,
#149126,#149127,#149128,#149129,#149130,#149131,#149132,#149133,#149134,
#149135,#149136,#149137,#149138,#149139,#149140,#149141,#149142,#149143,
#149144,#149145,#149146,#149147,#149148,#149149,#149150,#149151,#149152,
#149153,#149154,#149155,#149156,#149157,#149158,#149159,#149160,#149161,
#149162,#149163,#149164,#149165,#149166,#149167,#149168,#149169,#149170,
#149171,#149172,#149173,#149174,#149175,#149176,#149177,#149178,#149179,
#149180,#149181,#149182,#149183,#149184,#149185,#149186,#149187,#149188,
#149189,#149190,#149191,#149192,#149193,#149194,#149195,#149196,#149197,
#149198,#149199),.UNSPECIFIED.,.F.,.F.,(4,3,3,3,3,3,3,3,3,3,3,3,3,3,3,3,
3,3,3,3,3,3,3,3,3,3,3,3,3,3,3,3,3,3,3,3,3,3,3,3,3,4),(141.371669411768,
141.485016004534,141.600339367052,141.71566272957,141.814260854574,141.91271863735,
142.012941205123,142.111220762851,142.209467341925,142.307710424963,142.409407613605,
142.507792027024,142.611145603278,142.714499179532,142.813097304536,142.911555087312,
143.011777655085,143.110057212813,143.208303791887,143.306546874925,143.408244063567,
143.506628476986,143.60998205324,143.713335629494,143.811933754498,143.910391537274,
144.010614105047,144.108893662775,144.207140241849,144.305383324887,144.407080513529,
144.505464926948,144.608818503202,144.712172079456,144.81074660183,144.909191401417,
145.007536191857,145.105810581995,145.204060790383,145.302298022116,145.400579631087,
145.428467348202),.UNSPECIFIED.);
#1558=B_SPLINE_CURVE_WITH_KNOTS('',3,(#149200,#149201,#149202,#149203,#149204,
#149205,#149206,#149207,#149208,#149209,#149210,#149211,#149212,#149213,
#149214,#149215,#149216,#149217,#149218,#149219,#149220,#149221,#149222,
#149223,#149224,#149225,#149226,#149227,#149228,#149229,#149230,#149231,
#149232,#149233,#149234,#149235,#149236,#149237,#149238,#149239,#149240,
#149241,#149242,#149243,#149244,#149245,#149246,#149247,#149248,#149249,
#149250,#149251,#149252,#149253,#149254,#149255,#149256,#149257,#149258,
#149259,#149260,#149261,#149262,#149263,#149264,#149265,#149266,#149267,
#149268,#149269),.UNSPECIFIED.,.F.,.F.,(4,3,3,3,3,3,3,3,3,3,3,3,3,3,3,3,
3,3,3,3,3,3,3,4),(139.14605062869,139.244292891595,139.342541058438,139.440891113436,
139.539292964499,139.637867616823,139.717989829646,139.81658795465,139.915045737426,
140.015268305199,140.113547862927,140.211794442001,140.310037525039,140.411734713681,
140.5101191271,140.613472703354,140.716826279608,140.815569227393,140.914173010821,
141.012667061738,141.11108183093,141.209449097701,141.307822396311,141.371669411541),
 .UNSPECIFIED.);
#1559=B_SPLINE_CURVE_WITH_KNOTS('',3,(#149271,#149272,#149273,#149274,#149275,
#149276,#149277),.UNSPECIFIED.,.F.,.F.,(4,1,1,1,4),(139.145213405918,139.253183097127,
140.252019547089,141.250855997051,141.371669411541),.UNSPECIFIED.);
#1560=B_SPLINE_CURVE_WITH_KNOTS('',3,(#149278,#149279,#149280,#149281,#149282,
#149283,#149284,#149285,#149286,#149287,#149288,#149289,#149290,#149291,
#149292,#149293,#149294,#149295,#149296,#149297,#149298,#149299,#149300,
#149301,#149302,#149303,#149304,#149305,#149306,#149307,#149308,#149309,
#149310,#149311,#149312,#149313,#149314,#149315,#149316,#149317,#149318,
#149319,#149320,#149321,#149322,#149323,#149324,#149325,#149326,#149327,
#149328,#149329,#149330,#149331,#149332,#149333,#149334,#149335,#149336,
#149337,#149338,#149339,#149340,#149341,#149342,#149343,#149344,#149345,
#149346,#149347,#149348,#149349,#149350,#149351,#149352,#149353,#149354,
#149355,#149356,#149357,#149358,#149359,#149360,#149361,#149362,#149363,
#149364,#149365,#149366,#149367,#149368,#149369,#149370,#149371,#149372,
#149373,#149374,#149375,#149376,#149377,#149378,#149379,#149380,#149381,
#149382,#149383,#149384,#149385,#149386,#149387,#149388,#149389,#149390,
#149391,#149392,#149393,#149394,#149395,#149396,#149397,#149398,#149399,
#149400,#149401),.UNSPECIFIED.,.F.,.F.,(4,3,3,3,3,3,3,3,3,3,3,3,3,3,3,3,
3,3,3,3,3,3,3,3,3,3,3,3,3,3,3,3,3,3,3,3,3,3,3,3,3,4),(141.371669411541,
141.468831254161,141.566438903267,141.66339620349,141.760311911022,141.857216996242,
141.955335858934,142.052368429038,142.151030438025,142.249692447012,142.348290572016,
142.446748354792,142.546970922565,142.645250480293,142.743497059366,142.841740142405,
142.943437331047,143.041821744466,143.14517532072,143.248528896974,143.347127021978,
143.445584804755,143.545807372527,143.644086930255,143.742333509329,143.840576592367,
143.942273781009,144.040658194428,144.144011770682,144.247365346936,144.34596347194,
144.444421254716,144.544643822489,144.642923380217,144.74116995929,144.839413042329,
144.941110230971,145.03949464439,145.142848220644,145.246201796898,145.344774861151,
145.429604694147),.UNSPECIFIED.);
#1561=B_SPLINE_CURVE_WITH_KNOTS('',3,(#149407,#149408,#149409,#149410,#149411,
#149412,#149413,#149414,#149415),.UNSPECIFIED.,.F.,.F.,(4,1,1,1,1,1,4),
(147.65485471872,147.708681429341,148.707517879303,149.706354329265,150.705190779227,
151.704027229189,151.712252778999),.UNSPECIFIED.);
#1562=B_SPLINE_CURVE_WITH_KNOTS('',3,(#149416,#149417,#149418,#149419,#149420,
#149421,#149422,#149423,#149424,#149425,#149426,#149427,#149428,#149429,
#149430,#149431,#149432,#149433,#149434,#149435,#149436,#149437,#149438,
#149439,#149440,#149441,#149442,#149443,#149444,#149445,#149446,#149447,
#149448,#149449,#149450,#149451,#149452,#149453,#149454,#149455,#149456,
#149457,#149458,#149459,#149460,#149461,#149462,#149463,#149464,#149465,
#149466,#149467,#149468,#149469,#149470,#149471,#149472,#149473,#149474,
#149475,#149476,#149477,#149478,#149479,#149480,#149481,#149482,#149483,
#149484,#149485),.UNSPECIFIED.,.F.,.F.,(4,3,3,3,3,3,3,3,3,3,3,3,3,3,3,3,
3,3,3,3,3,3,3,4),(145.428467348202,145.52686564106,145.625438462383,145.711008529418,
145.809606654422,145.908064437198,146.008287004971,146.106566562699,146.204813141772,
146.303056224811,146.404753413453,146.503137826872,146.606491403125,146.709844979379,
146.807643480436,146.905302408374,147.002849316603,147.100335701354,147.197792033696,
147.295248746519,147.3927980835,147.490396206244,147.588155506493,147.65485471872),
 .UNSPECIFIED.);
#1563=B_SPLINE_CURVE_WITH_KNOTS('',3,(#149487,#149488,#149489,#149490,#149491,
#149492,#149493,#149494,#149495,#149496,#149497,#149498,#149499,#149500,
#149501,#149502,#149503,#149504,#149505,#149506,#149507,#149508,#149509,
#149510,#149511,#149512,#149513,#149514,#149515,#149516,#149517,#149518,
#149519,#149520,#149521,#149522,#149523,#149524,#149525,#149526,#149527,
#149528,#149529,#149530,#149531,#149532,#149533,#149534,#149535,#149536,
#149537,#149538,#149539,#149540,#149541,#149542,#149543,#149544,#149545,
#149546,#149547,#149548,#149549,#149550,#149551,#149552,#149553,#149554,
#149555,#149556),.UNSPECIFIED.,.F.,.F.,(4,3,3,3,3,3,3,3,3,3,3,3,3,3,3,3,
3,3,3,3,3,3,3,4),(145.429604694147,145.531533888236,145.629819464068,145.728068476452,
145.826310411335,145.924574738934,146.022950488803,146.121392854414,146.219991618488,
146.24503824686,146.343636371864,146.442094154641,146.542316722413,146.640596280141,
146.738842859215,146.837085942253,146.938783130895,147.037167544314,147.140521120568,
147.243874696822,147.352569174392,147.460952550046,147.568802109382,147.654854305399),
 .UNSPECIFIED.);
#1564=B_SPLINE_CURVE_WITH_KNOTS('',3,(#149557,#149558,#149559,#149560,#149561,
#149562,#149563,#149564),.UNSPECIFIED.,.F.,.F.,(4,1,1,1,1,4),(147.65485471872,
148.242711146784,149.241547596746,150.240384046707,151.239220496669,151.712342700426),
 .UNSPECIFIED.);
#1565=B_SPLINE_CURVE_WITH_KNOTS('',3,(#149570,#149571,#149572,#149573,#149574,
#149575,#149576,#149577,#149578,#149579,#149580,#149581,#149582,#149583,
#149584,#149585,#149586,#149587,#149588,#149589,#149590,#149591,#149592,
#149593,#149594,#149595,#149596,#149597,#149598,#149599,#149600,#149601,
#149602,#149603,#149604,#149605,#149606,#149607,#149608,#149609,#149610,
#149611,#149612,#149613,#149614,#149615,#149616,#149617,#149618,#149619,
#149620,#149621,#149622,#149623,#149624,#149625,#149626,#149627,#149628,
#149629,#149630,#149631,#149632,#149633,#149634,#149635,#149636,#149637,
#149638,#149639,#149640,#149641,#149642,#149643,#149644,#149645,#149646,
#149647,#149648,#149649,#149650,#149651,#149652,#149653,#149654,#149655,
#149656,#149657,#149658,#149659,#149660,#149661,#149662,#149663,#149664,
#149665,#149666,#149667,#149668,#149669,#149670,#149671,#149672,#149673,
#149674,#149675,#149676,#149677,#149678,#149679,#149680,#149681,#149682,
#149683,#149684,#149685,#149686,#149687,#149688,#149689,#149690,#149691,
#149692,#149693),.UNSPECIFIED.,.F.,.F.,(4,3,3,3,3,3,3,3,3,3,3,3,3,3,3,3,
3,3,3,3,3,3,3,3,3,3,3,3,3,3,3,3,3,3,3,3,3,3,3,3,3,4),(153.9380400259,154.035163898234,
154.132222574363,154.229246955324,154.326267897773,154.423381488606,154.520541056366,
154.617870832504,154.700536579074,154.799134704076,154.897592486852,154.997815054625,
155.096094612352,155.194341191424,155.292584274461,155.394281463105,155.492665876523,
155.596019452779,155.699373029036,155.797971154037,155.896428936811,155.996651504585,
156.09493106231,156.193177641381,156.291420724416,156.393117913062,156.491502326478,
156.594855902738,156.698209478998,156.796807604012,156.895265386799,156.995487954569,
157.093767512308,157.192014091392,157.29025717444,157.39195436307,157.490338776499,
157.59369235273,157.69704592896,157.795632129848,157.895770619144,157.995909108439),
 .UNSPECIFIED.);
#1566=B_SPLINE_CURVE_WITH_KNOTS('',3,(#149694,#149695,#149696,#149697,#149698,
#149699),.UNSPECIFIED.,.F.,.F.,(4,1,1,4),(151.712252778999,152.702863679151,
153.701700129113,153.938039726298),.UNSPECIFIED.);
#1567=B_SPLINE_CURVE_WITH_KNOTS('',3,(#149701,#149702,#149703,#149704,#149705,
#149706),.UNSPECIFIED.,.F.,.F.,(4,1,1,4),(151.712342700426,152.238056946631,
153.236893396593,153.9380400259),.UNSPECIFIED.);
#1568=B_SPLINE_CURVE_WITH_KNOTS('',3,(#149707,#149708,#149709,#149710,#149711,
#149712,#149713,#149714,#149715,#149716,#149717,#149718,#149719,#149720,
#149721,#149722,#149723,#149724,#149725,#149726,#149727,#149728,#149729,
#149730,#149731,#149732,#149733,#149734,#149735,#149736,#149737,#149738,
#149739,#149740,#149741,#149742,#149743,#149744,#149745,#149746,#149747,
#149748,#149749,#149750,#149751,#149752,#149753,#149754,#149755,#149756,
#149757,#149758,#149759,#149760,#149761,#149762,#149763,#149764,#149765,
#149766,#149767,#149768,#149769,#149770,#149771,#149772,#149773,#149774,
#149775,#149776,#149777,#149778,#149779,#149780,#149781,#149782,#149783,
#149784,#149785,#149786,#149787,#149788,#149789,#149790,#149791,#149792,
#149793,#149794,#149795,#149796,#149797,#149798,#149799,#149800,#149801,
#149802,#149803,#149804,#149805,#149806,#149807,#149808,#149809,#149810,
#149811,#149812,#149813,#149814,#149815,#149816,#149817,#149818,#149819,
#149820,#149821,#149822,#149823,#149824,#149825,#149826,#149827,#149828,
#149829,#149830),.UNSPECIFIED.,.F.,.F.,(4,3,3,3,3,3,3,3,3,3,3,3,3,3,3,3,
3,3,3,3,3,3,3,3,3,3,3,3,3,3,3,3,3,3,3,3,3,3,3,3,3,4),(153.938040202766,
154.056659980235,154.176963650991,154.235729846555,154.334327971559,154.432785754335,
154.533008322108,154.631287879836,154.729534458909,154.827777541948,154.92947473059,
155.027859144009,155.131212720263,155.234566296517,155.33316442152,155.431622204297,
155.531844772069,155.630124329797,155.72837090887,155.826613991908,155.928311180551,
156.026695593969,156.130049170224,156.233402746479,156.332000871484,156.430458654262,
156.530681222035,156.628960779764,156.727207358839,156.825450441879,156.927147630519,
157.025532043939,157.12888562019,157.232239196441,157.330809964381,157.429252216959,
157.527595662268,157.625869905303,157.724128943532,157.822375482215,157.920688283613,
157.994794053202),.UNSPECIFIED.);
#1569=B_SPLINE_CURVE_WITH_KNOTS('',3,(#149836,#149837,#149838,#149839,#149840,
#149841,#149842,#149843),.UNSPECIFIED.,.F.,.F.,(4,1,1,1,1,4),(160.221227414878,
160.693555278846,161.692391728808,162.691228178769,163.690064628731,164.278110100501),
 .UNSPECIFIED.);
#1570=B_SPLINE_CURVE_WITH_KNOTS('',3,(#149844,#149845,#149846,#149847,#149848,
#149849,#149850,#149851,#149852,#149853,#149854,#149855,#149856,#149857,
#149858,#149859,#149860,#149861,#149862,#149863,#149864,#149865,#149866,
#149867,#149868,#149869,#149870,#149871,#149872,#149873,#149874,#149875,
#149876,#149877,#149878,#149879,#149880,#149881,#149882,#149883,#149884,
#149885,#149886,#149887,#149888,#149889,#149890,#149891,#149892,#149893,
#149894,#149895,#149896,#149897,#149898,#149899,#149900,#149901,#149902,
#149903,#149904,#149905,#149906,#149907,#149908,#149909,#149910,#149911,
#149912,#149913),.UNSPECIFIED.,.F.,.F.,(4,3,3,3,3,3,3,3,3,3,3,3,3,3,3,3,
3,3,3,3,3,3,3,4),(157.995909108439,158.094187900561,158.192434189533,158.290677457562,
158.391978687902,158.490363797708,158.593123088315,158.695882378922,158.794480503912,
158.892938286675,158.993160854451,159.091440412165,159.189686991224,159.287930074248,
159.389627262907,159.488011676311,159.591365252598,159.694718828884,159.797216560019,
159.903218753284,160.005303397592,160.107256278837,160.209067828956,160.22122533308),
 .UNSPECIFIED.);
#1571=B_SPLINE_CURVE_WITH_KNOTS('',3,(#149915,#149916,#149917,#149918,#149919,
#149920,#149921,#149922,#149923,#149924,#149925,#149926,#149927,#149928,
#149929,#149930,#149931,#149932,#149933,#149934,#149935,#149936,#149937,
#149938,#149939,#149940,#149941,#149942,#149943,#149944,#149945,#149946,
#149947,#149948,#149949,#149950,#149951,#149952,#149953,#149954,#149955,
#149956,#149957,#149958,#149959,#149960,#149961,#149962,#149963,#149964,
#149965,#149966,#149967,#149968,#149969,#149970,#149971,#149972,#149973,
#149974,#149975,#149976,#149977,#149978,#149979,#149980,#149981,#149982,
#149983,#149984),.UNSPECIFIED.,.F.,.F.,(4,3,3,3,3,3,3,3,3,3,3,3,3,3,3,3,
3,3,3,3,3,3,3,4),(157.994794053202,158.093225172905,158.191816739594,158.231075646402,
158.329673771403,158.428131554177,158.528354121951,158.626633679676,158.724880258747,
158.823123341783,158.924820530428,159.023204943844,159.126558520104,159.229912096364,
159.328378576654,159.426704810661,159.526019875932,159.624169149678,159.722285836342,
159.820399593048,159.920606027993,160.018861091251,160.120043212039,160.221225332828),
 .UNSPECIFIED.);
#1572=B_SPLINE_CURVE_WITH_KNOTS('',3,(#149985,#149986,#149987,#149988,#149989,
#149990,#149991,#149992,#149993,#149994,#149995,#149996,#149997,#149998,
#149999,#150000,#150001,#150002,#150003,#150004,#150005,#150006,#150007,
#150008,#150009,#150010,#150011,#150012,#150013,#150014,#150015,#150016,
#150017,#150018,#150019,#150020,#150021,#150022,#150023,#150024,#150025,
#150026,#150027,#150028,#150029,#150030,#150031,#150032,#150033,#150034,
#150035,#150036,#150037,#150038,#150039,#150040,#150041,#150042,#150043,
#150044,#150045,#150046,#150047,#150048,#150049,#150050,#150051,#150052,
#150053,#150054,#150055,#150056,#150057,#150058,#150059,#150060,#150061,
#150062,#150063,#150064,#150065,#150066,#150067,#150068,#150069,#150070,
#150071,#150072,#150073,#150074,#150075,#150076,#150077,#150078,#150079,
#150080,#150081,#150082,#150083,#150084,#150085,#150086,#150087,#150088,
#150089,#150090,#150091,#150092,#150093,#150094,#150095,#150096,#150097,
#150098,#150099,#150100,#150101,#150102,#150103,#150104,#150105,#150106,
#150107,#150108,#150109,#150110,#150111),.UNSPECIFIED.,.F.,.F.,(4,3,3,3,
3,3,3,3,3,3,3,3,3,3,3,3,3,3,3,3,3,3,3,3,3,3,3,3,3,3,3,3,3,3,3,3,3,3,3,3,
3,3,4),(160.22122533308,160.228748546326,160.327346671318,160.425804454083,
160.526027021859,160.624306579575,160.722553158637,160.820796241665,160.92249343032,
161.020877843728,161.124231420008,161.227584996288,161.326183121278,161.424640904041,
161.524863471817,161.623143029531,161.72138960859,161.819632691615,161.921329880273,
162.019714293678,162.123067869964,162.22642144625,162.325019571326,162.423477354175,
162.52369992193,162.62197947973,162.720226058876,162.818469141986,162.920166330542,
163.018550744032,163.121904320122,163.225257896212,163.323856021116,163.422313803793,
163.522536371591,163.620815929221,163.719062508197,163.817305591139,163.919002779898,
164.017387193223,164.120740769699,164.224094346174,164.278857765994),
 .UNSPECIFIED.);
#1573=B_SPLINE_CURVE_WITH_KNOTS('',3,(#150117,#150118,#150119,#150120,#150121,
#150122,#150123,#150124,#150125,#150126,#150127,#150128,#150129,#150130,
#150131,#150132,#150133,#150134,#150135,#150136,#150137,#150138,#150139,
#150140,#150141,#150142,#150143,#150144,#150145,#150146,#150147,#150148,
#150149,#150150,#150151,#150152,#150153,#150154,#150155,#150156,#150157,
#150158,#150159,#150160,#150161,#150162,#150163,#150164,#150165,#150166,
#150167,#150168,#150169,#150170,#150171,#150172,#150173,#150174,#150175,
#150176,#150177,#150178,#150179,#150180,#150181,#150182,#150183,#150184,
#150185,#150186,#150187,#150188,#150189,#150190,#150191,#150192,#150193,
#150194,#150195,#150196,#150197,#150198,#150199,#150200,#150201,#150202,
#150203,#150204,#150205,#150206,#150207,#150208,#150209,#150210,#150211,
#150212,#150213,#150214,#150215,#150216,#150217,#150218,#150219,#150220,
#150221,#150222,#150223,#150224,#150225,#150226,#150227,#150228,#150229,
#150230,#150231,#150232,#150233,#150234,#150235,#150236,#150237,#150238,
#150239,#150240),.UNSPECIFIED.,.F.,.F.,(4,3,3,3,3,3,3,3,3,3,3,3,3,3,3,3,
3,3,3,3,3,3,3,3,3,3,3,3,3,3,3,3,3,3,3,3,3,3,3,3,3,4),(166.504410640259,
166.652910770227,166.686573978617,166.785172097216,166.883629873594,166.983852442967,
167.082131994355,167.180378567125,167.278621643903,167.380318840072,167.478703247402,
167.58205683799,167.685410428579,167.784008554554,167.882466338243,167.98268890578,
168.080968464272,168.179215044053,168.277458127742,168.379155315442,168.477539729364,
168.580893303952,168.684246878541,168.782845025293,168.881302829919,168.981525392242,
169.079804971909,169.178051572908,169.276294677829,169.377991840497,169.476376275469,
169.579729801986,169.683083328503,169.781689727945,169.880127484649,169.978469449795,
170.076745219903,170.174984320903,170.273261950043,170.371554712591,170.469968413607,
170.561255441754),.UNSPECIFIED.);
#1574=B_SPLINE_CURVE_WITH_KNOTS('',3,(#150241,#150242,#150243,#150244,#150245,
#150246),.UNSPECIFIED.,.F.,.F.,(4,1,1,4),(164.278110100501,164.688901078693,
165.687737528655,166.504405683232),.UNSPECIFIED.);
#1575=B_SPLINE_CURVE_WITH_KNOTS('',3,(#150248,#150249,#150250,#150251,#150252,
#150253,#150254,#150255,#150256,#150257,#150258,#150259,#150260,#150261,
#150262,#150263,#150264,#150265,#150266,#150267,#150268,#150269,#150270,
#150271,#150272,#150273,#150274,#150275,#150276,#150277,#150278,#150279,
#150280,#150281,#150282,#150283,#150284,#150285,#150286,#150287,#150288,
#150289,#150290,#150291,#150292,#150293,#150294,#150295,#150296,#150297,
#150298,#150299,#150300,#150301,#150302,#150303,#150304,#150305,#150306,
#150307,#150308,#150309,#150310,#150311,#150312,#150313,#150314,#150315,
#150316,#150317),.UNSPECIFIED.,.F.,.F.,(4,3,3,3,3,3,3,3,3,3,3,3,3,3,3,3,
3,3,3,3,3,3,3,4),(164.278857765994,164.377373907485,164.475767948866,164.574072822073,
164.672331029923,164.770572069846,164.868825414456,164.967184460474,165.065601054055,
165.164183854236,165.222930796136,165.321528921635,165.419986704909,165.520209272558,
165.618488830783,165.716735410353,165.814978493886,165.916675681939,166.015060095843,
166.11841367097,166.221767246097,166.34459987441,166.465474953157,166.504410639987),
 .UNSPECIFIED.);
#1576=B_SPLINE_CURVE_WITH_KNOTS('',3,(#150318,#150319,#150320,#150321,#150322,
#150323,#150324,#150325,#150326,#150327,#150328,#150329,#150330,#150331,
#150332,#150333,#150334,#150335,#150336,#150337,#150338,#150339,#150340,
#150341,#150342,#150343,#150344,#150345,#150346,#150347,#150348,#150349,
#150350,#150351,#150352,#150353,#150354,#150355,#150356,#150357,#150358,
#150359,#150360,#150361,#150362,#150363,#150364,#150365,#150366,#150367,
#150368,#150369,#150370,#150371,#150372,#150373,#150374,#150375,#150376,
#150377,#150378,#150379,#150380,#150381,#150382,#150383,#150384,#150385,
#150386,#150387,#150388,#150389,#150390,#150391,#150392,#150393,#150394,
#150395,#150396,#150397,#150398,#150399,#150400,#150401,#150402,#150403,
#150404,#150405,#150406,#150407,#150408,#150409,#150410,#150411,#150412,
#150413,#150414,#150415,#150416,#150417,#150418,#150419,#150420,#150421,
#150422,#150423,#150424,#150425,#150426,#150427,#150428,#150429,#150430,
#150431,#150432,#150433,#150434,#150435,#150436,#150437,#150438,#150439,
#150440,#150441,#150442,#150443,#150444),.UNSPECIFIED.,.F.,.F.,(4,3,3,3,
3,3,3,3,3,3,3,3,3,3,3,3,3,3,3,3,3,3,3,3,3,3,3,3,3,3,3,3,3,3,3,3,3,3,3,3,
3,3,4),(166.504410640259,166.6019131263,166.699371433809,166.79681599036,
166.894277201724,166.991846173228,167.089478292237,167.187269535439,167.220603696059,
167.319201820915,167.417659603535,167.517882171346,167.616161728898,167.714408307788,
167.812651390637,167.914348579483,168.012732992698,168.116086569359,168.219440146021,
168.318038274346,168.416496060457,168.516718627398,168.614998188467,168.713244770876,
168.811487857242,168.913185041927,169.011569458616,169.1149230273,169.218276595983,
169.316874714607,169.415332491011,169.515555060377,169.613834611791,169.712081184585,
169.810324261387,169.912021457527,170.01040586488,170.113759455413,170.217113045945,
170.315689889885,170.414143809233,170.512486666531,170.562190678317),
 .UNSPECIFIED.);
#1577=B_SPLINE_CURVE_WITH_KNOTS('',3,(#150450,#150451,#150452,#150453,#150454,
#150455,#150456,#150457,#150458,#150459,#150460,#150461,#150462,#150463,
#150464,#150465,#150466,#150467,#150468,#150469,#150470,#150471,#150472,
#150473,#150474,#150475,#150476,#150477,#150478,#150479,#150480,#150481,
#150482,#150483,#150484,#150485,#150486,#150487,#150488,#150489,#150490,
#150491,#150492,#150493,#150494,#150495,#150496,#150497,#150498,#150499,
#150500,#150501,#150502,#150503,#150504,#150505,#150506,#150507,#150508,
#150509,#150510,#150511,#150512,#150513,#150514,#150515,#150516,#150517,
#150518,#150519,#150520,#150521,#150522,#150523,#150524,#150525,#150526,
#150527,#150528,#150529,#150530,#150531,#150532,#150533,#150534,#150535,
#150536,#150537,#150538,#150539,#150540,#150541,#150542,#150543,#150544,
#150545,#150546,#150547,#150548,#150549,#150550,#150551,#150552,#150553,
#150554,#150555,#150556,#150557,#150558,#150559,#150560,#150561,#150562,
#150563,#150564,#150565,#150566,#150567,#150568,#150569,#150570,#150571,
#150572,#150573,#150574,#150575,#150576),.UNSPECIFIED.,.F.,.F.,(4,3,3,3,
3,3,3,3,3,3,3,3,3,3,3,3,3,3,3,3,3,3,3,3,3,3,3,3,3,3,3,3,3,3,3,3,3,3,3,3,
3,3,4),(172.787595947668,172.884841558603,172.984040004821,173.081071836984,
173.178059268517,173.275033212281,173.375882191298,173.472980624789,173.57014496826,
173.66745840562,173.67842912835,173.777027506535,173.875485539983,173.975708044774,
174.073987845308,174.172234663756,174.270477982445,174.372174881412,174.470559518906,
174.573912548609,174.677265578312,174.77586453171,174.874323148858,174.974545508785,
175.072825909421,175.171073332739,175.26931726024,175.371013452249,175.469398702017,
175.572750365145,175.676102028274,175.774697485907,175.873152598171,175.973375833179,
176.071652731782,176.169896661679,176.2681371089,176.369837451234,176.468219288705,
176.57157888347,176.674938478236,176.773518528063,176.845520771701),
 .UNSPECIFIED.);
#1578=B_SPLINE_CURVE_WITH_KNOTS('',3,(#150577,#150578,#150579,#150580,#150581,
#150582,#150583,#150584,#150585,#150586,#150587,#150588,#150589,#150590,
#150591,#150592,#150593,#150594,#150595,#150596,#150597,#150598,#150599,
#150600,#150601,#150602,#150603,#150604,#150605,#150606,#150607,#150608,
#150609,#150610,#150611,#150612,#150613,#150614,#150615,#150616,#150617,
#150618,#150619,#150620,#150621,#150622,#150623,#150624,#150625,#150626,
#150627,#150628,#150629,#150630,#150631,#150632,#150633,#150634,#150635,
#150636,#150637,#150638,#150639,#150640,#150641,#150642,#150643,#150644,
#150645,#150646),.UNSPECIFIED.,.F.,.F.,(4,3,3,3,3,3,3,3,3,3,3,3,3,3,3,3,
3,3,3,3,3,3,3,4),(170.561255441754,170.659855757029,170.681919778464,170.780517924866,
170.878975728651,170.979198291123,171.077477868768,171.17572446731,171.273967569349,
171.375664734118,171.474049165187,171.577402696807,171.680756228426,171.779354490553,
171.877812411242,171.978034944635,172.076314641203,172.17456135916,172.272804580942,
172.374501605303,172.472886155702,172.576239417045,172.679592678388,172.787595947439),
 .UNSPECIFIED.);
#1579=B_SPLINE_CURVE_WITH_KNOTS('',3,(#150648,#150649,#150650,#150651,#150652,
#150653,#150654,#150655,#150656,#150657,#150658,#150659,#150660,#150661,
#150662,#150663,#150664,#150665,#150666,#150667,#150668,#150669,#150670,
#150671,#150672,#150673,#150674,#150675,#150676,#150677,#150678,#150679,
#150680,#150681,#150682,#150683,#150684,#150685,#150686,#150687,#150688,
#150689,#150690,#150691,#150692,#150693,#150694,#150695,#150696,#150697,
#150698,#150699,#150700,#150701,#150702,#150703,#150704,#150705,#150706,
#150707,#150708,#150709,#150710,#150711,#150712,#150713,#150714,#150715,
#150716,#150717),.UNSPECIFIED.,.F.,.F.,(4,3,3,3,3,3,3,3,3,3,3,3,3,3,3,3,
3,3,3,3,3,3,3,4),(170.562190678317,170.660450514926,170.758691713403,170.856943746971,
170.955300618973,171.053713717861,171.152294511815,171.215949495907,171.314547642568,
171.413005447104,171.51322800945,171.611507589026,171.709754189934,171.807997294764,
171.90969445754,172.008078892422,172.111432419146,172.214785945869,172.315617765325,
172.416285943672,172.516781875576,172.617176498836,172.717484580328,172.787595947439),
 .UNSPECIFIED.);
#1580=B_SPLINE_CURVE_WITH_KNOTS('',3,(#150718,#150719,#150720,#150721,#150722,
#150723,#150724,#150725),.UNSPECIFIED.,.F.,.F.,(4,1,1,1,1,4),(172.787601414694,
173.21362239583,174.212458845792,175.211295295754,176.210131745716,176.844282077012),
 .UNSPECIFIED.);
#1581=B_SPLINE_CURVE_WITH_KNOTS('',3,(#150731,#150732,#150733,#150734,#150735,
#150736,#150737,#150738),.UNSPECIFIED.,.F.,.F.,(4,1,1,1,1,4),(179.070781254618,
179.671447828121,180.670284278083,181.669120728045,182.667957178007,183.128402568106),
 .UNSPECIFIED.);
#1582=B_SPLINE_CURVE_WITH_KNOTS('',3,(#150739,#150740,#150741,#150742,#150743,
#150744,#150745,#150746,#150747,#150748,#150749,#150750,#150751,#150752,
#150753,#150754,#150755,#150756,#150757,#150758,#150759,#150760,#150761,
#150762,#150763,#150764,#150765,#150766,#150767,#150768,#150769,#150770,
#150771,#150772,#150773,#150774,#150775,#150776,#150777,#150778,#150779,
#150780,#150781,#150782,#150783,#150784,#150785,#150786,#150787,#150788,
#150789,#150790,#150791,#150792,#150793,#150794,#150795,#150796,#150797,
#150798,#150799,#150800,#150801,#150802,#150803,#150804,#150805,#150806,
#150807,#150808),.UNSPECIFIED.,.F.,.F.,(4,3,3,3,3,3,3,3,3,3,3,3,3,3,3,3,
3,3,3,3,3,3,3,4),(176.845520771701,176.949052541263,177.047346590345,177.145600683284,
177.243844306548,177.342106927815,177.440479043576,177.538914719441,177.637509918042,
177.673774928198,177.772377764499,177.870840302866,177.971061687278,178.069346073991,
178.167597498754,178.265845437705,178.367536922818,178.465926167544,178.569268772851,
178.672611378159,178.782250111505,178.891545462336,179.000249339659,179.070781030153),
 .UNSPECIFIED.);
#1583=B_SPLINE_CURVE_WITH_KNOTS('',3,(#150810,#150811,#150812,#150813,#150814,
#150815),.UNSPECIFIED.,.F.,.F.,(4,1,1,4),(176.844282077012,177.208968195678,
178.20780464564,179.070781254618),.UNSPECIFIED.);
#1584=B_SPLINE_CURVE_WITH_KNOTS('',3,(#150816,#150817,#150818,#150819,#150820,
#150821,#150822,#150823),.UNSPECIFIED.,.F.,.F.,(4,1,1,1,1,4),(179.070781254618,
179.206641095602,180.205477545564,181.204313995525,182.203150445487,183.127688302604),
 .UNSPECIFIED.);
#1585=B_SPLINE_CURVE_WITH_KNOTS('',3,(#150829,#150830,#150831,#150832,#150833,
#150834,#150835,#150836),.UNSPECIFIED.,.F.,.F.,(4,1,1,1,1,4),(15.707963267949,
15.8622700343739,16.8611064843358,17.8599429342977,18.8587793842596,19.7647622867482),
 .UNSPECIFIED.);
#1586=B_SPLINE_CURVE_WITH_KNOTS('',3,(#150838,#150839,#150840,#150841,#150842,
#150843,#150844,#150845,#150846,#150847,#150848,#150849,#150850,#150851,
#150852,#150853,#150854,#150855,#150856,#150857,#150858,#150859,#150860,
#150861,#150862,#150863,#150864,#150865,#150866,#150867,#150868,#150869,
#150870,#150871,#150872,#150873,#150874,#150875,#150876,#150877,#150878,
#150879,#150880,#150881,#150882,#150883,#150884,#150885,#150886,#150887,
#150888,#150889,#150890,#150891,#150892,#150893,#150894,#150895),
 .UNSPECIFIED.,.F.,.F.,(4,3,3,3,3,3,3,3,3,3,3,3,3,3,3,3,3,3,3,4),(13.8757070305535,
13.9742334885845,14.0726196430263,14.1714713856996,14.2696800147309,14.3678555358064,
14.4660275256487,14.5653790403396,14.6636889428954,14.7635612636538,14.8634335844121,
14.9606976643214,15.0578044061946,15.154822904629,15.2517842090804,15.3487192963901,
15.4457083601634,15.5427241599104,15.6398692512359,15.707963267949),
 .UNSPECIFIED.);
#1587=B_SPLINE_CURVE_WITH_KNOTS('',3,(#150899,#150900,#150901,#150902,#150903),
 .UNSPECIFIED.,.F.,.F.,(4,1,4),(14.3986268518925,15.3974633018543,15.707963267949),
 .UNSPECIFIED.);
#1588=B_SPLINE_CURVE_WITH_KNOTS('',3,(#150904,#150905,#150906,#150907,#150908,
#150909,#150910,#150911),.UNSPECIFIED.,.F.,.F.,(4,1,1,1,1,4),(15.707963267949,
16.3962997518162,17.3951362017781,18.39397265174,19.3928091017018,19.7659327146509),
 .UNSPECIFIED.);
#1589=B_SPLINE_CURVE_WITH_KNOTS('',3,(#150917,#150918,#150919,#150920,#150921,
#150922,#150923,#150924),.UNSPECIFIED.,.F.,.F.,(4,1,1,1,1,4),(21.9911485751286,
22.854125184107,23.8529616340689,24.8517980840308,25.8506345339927,26.0493850218968),
 .UNSPECIFIED.);
#1590=B_SPLINE_CURVE_WITH_KNOTS('',3,(#150925,#150926,#150927,#150928,#150929,
#150930,#150931),.UNSPECIFIED.,.F.,.F.,(4,1,1,1,4),(19.7647622867482,19.8576158342214,
20.8564522841833,21.8552887341452,21.9911485751286),.UNSPECIFIED.);
#1591=B_SPLINE_CURVE_WITH_KNOTS('',3,(#150933,#150934,#150935,#150936,#150937,
#150938),.UNSPECIFIED.,.F.,.F.,(4,1,1,4),(19.7659327146509,20.3916455516637,
21.3904820016256,21.9911485751286),.UNSPECIFIED.);
#1592=B_SPLINE_CURVE_WITH_KNOTS('',3,(#150939,#150940,#150941,#150942,#150943,
#150944,#150945,#150946,#150947,#150948,#150949,#150950,#150951,#150952,
#150953,#150954,#150955,#150956,#150957,#150958,#150959,#150960,#150961,
#150962,#150963,#150964,#150965,#150966,#150967,#150968,#150969,#150970,
#150971,#150972,#150973,#150974,#150975,#150976,#150977,#150978,#150979,
#150980,#150981,#150982,#150983,#150984,#150985,#150986,#150987,#150988,
#150989,#150990,#150991,#150992,#150993,#150994,#150995,#150996,#150997,
#150998,#150999,#151000,#151001,#151002,#151003,#151004,#151005,#151006,
#151007,#151008,#151009,#151010,#151011,#151012,#151013,#151014,#151015,
#151016,#151017,#151018,#151019,#151020,#151021,#151022,#151023,#151024,
#151025,#151026,#151027,#151028,#151029,#151030,#151031,#151032,#151033,
#151034,#151035,#151036,#151037,#151038,#151039,#151040,#151041,#151042,
#151043,#151044,#151045,#151046,#151047,#151048,#151049,#151050,#151051,
#151052,#151053,#151054,#151055,#151056,#151057,#151058,#151059,#151060,
#151061,#151062),.UNSPECIFIED.,.F.,.F.,(4,3,3,3,3,3,3,3,3,3,3,3,3,3,3,3,
3,3,3,3,3,3,3,3,3,3,3,3,3,3,3,3,3,3,3,3,3,3,3,3,3,4),(21.9911487995909,
22.0999040367044,22.2090425458686,22.3187160667875,22.3893184515875,22.487921335874,
22.5863839114419,22.6866052852053,22.7848896824335,22.883141107753,22.9813890373116,
23.0830805033711,23.1814697140479,23.2848123077986,23.3881549015493,23.4867551965745,
23.5852152014032,23.6854372201667,23.78371911203,23.8819680620747,23.9802135499039,
24.0819080003058,24.1802948788303,24.2836431151707,24.3869913515112,24.4855869755136,
24.5840422190559,24.6842654168581,24.7825423598393,24.8807863016633,24.9790267283841,
25.0807269966564,25.1791087331383,25.2824682673057,25.3858278014731,25.4844081060613,
25.5828572825197,25.6812050501617,25.7794880251905,25.8777310360909,25.9759959181972,
26.0480411834147),.UNSPECIFIED.);
#1593=B_SPLINE_CURVE_WITH_KNOTS('',3,(#151068,#151069,#151070,#151071,#151072,
#151073,#151074,#151075,#151076,#151077,#151078,#151079,#151080,#151081,
#151082,#151083,#151084,#151085,#151086,#151087,#151088,#151089,#151090,
#151091,#151092,#151093,#151094,#151095,#151096,#151097,#151098,#151099,
#151100,#151101,#151102,#151103,#151104,#151105,#151106,#151107,#151108,
#151109,#151110,#151111,#151112,#151113,#151114,#151115,#151116,#151117,
#151118,#151119,#151120,#151121,#151122,#151123,#151124,#151125,#151126,
#151127,#151128,#151129,#151130,#151131,#151132,#151133,#151134,#151135,
#151136,#151137,#151138,#151139,#151140,#151141,#151142,#151143,#151144,
#151145,#151146,#151147,#151148,#151149,#151150,#151151,#151152,#151153,
#151154,#151155,#151156,#151157,#151158,#151159,#151160,#151161,#151162,
#151163,#151164,#151165,#151166,#151167,#151168,#151169,#151170,#151171,
#151172,#151173,#151174,#151175,#151176,#151177,#151178,#151179,#151180,
#151181,#151182,#151183,#151184,#151185,#151186,#151187,#151188,#151189,
#151190,#151191),.UNSPECIFIED.,.F.,.F.,(4,3,3,3,3,3,3,3,3,3,3,3,3,3,3,3,
3,3,3,3,3,3,3,3,3,3,3,3,3,3,3,3,3,3,3,3,3,3,3,3,3,4),(28.2743338823082,
28.3746245107026,28.4749734040128,28.5754886322331,28.6760922705589,28.7769068627545,
28.8471438838783,28.9457420299255,29.0441998339908,29.144422396472,29.2427019759347,
29.3409485768614,29.4391916818436,29.5408888448427,29.6392732802058,29.742626807023,
29.8459803338402,29.9445784592274,30.043036242454,30.1432588101225,30.241538368462,
30.3397849482058,30.4380280319734,30.5397252199305,30.638109634218,30.74146320901,
30.844816783802,30.9434149029218,31.0418726797114,31.142095248968,31.2403748004981,
31.3386213733082,31.4368644500261,31.5385616459606,31.6369460529803,31.7402996433721,
31.8436532337639,31.9422528703178,32.0406907036715,32.1390337581138,32.2373181769772,
32.331714743168),.UNSPECIFIED.);
#1594=B_SPLINE_CURVE_WITH_KNOTS('',3,(#151192,#151193,#151194,#151195,#151196,
#151197),.UNSPECIFIED.,.F.,.F.,(4,1,1,4),(26.0493850218968,26.8494709839545,
27.8483074339164,28.2743284148783),.UNSPECIFIED.);
#1595=B_SPLINE_CURVE_WITH_KNOTS('',3,(#151199,#151200,#151201,#151202,#151203,
#151204,#151205,#151206,#151207,#151208,#151209,#151210,#151211,#151212,
#151213,#151214,#151215,#151216,#151217,#151218,#151219,#151220,#151221,
#151222,#151223,#151224,#151225,#151226,#151227,#151228,#151229,#151230,
#151231,#151232,#151233,#151234,#151235,#151236,#151237,#151238,#151239,
#151240,#151241,#151242,#151243,#151244,#151245,#151246,#151247,#151248,
#151249,#151250,#151251,#151252,#151253,#151254,#151255,#151256,#151257,
#151258,#151259,#151260,#151261,#151262,#151263,#151264,#151265,#151266,
#151267,#151268,#151269,#151270,#151271),.UNSPECIFIED.,.F.,.F.,(4,3,3,3,
3,3,3,3,3,3,3,3,3,3,3,3,3,3,3,3,3,3,3,3,4),(26.0480411834147,26.1464093623878,
26.244839798522,26.3434312469923,26.384664251435,26.4832625890263,26.5817205904922,
26.6819431043553,26.7802228942346,26.8784697099906,26.976713033946,27.0784099508087,
27.1767946133168,27.2801476573568,27.3835007013968,27.4808124349029,27.5800026158,
27.6770619108145,27.7740624128206,27.8710350559302,27.9718597624675,28.0689211605358,
28.1660361013683,28.2632831488084,28.2743338820795),.UNSPECIFIED.);
#1596=B_SPLINE_CURVE_WITH_KNOTS('',3,(#151272,#151273,#151274,#151275,#151276,
#151277,#151278,#151279,#151280,#151281,#151282,#151283,#151284,#151285,
#151286,#151287,#151288,#151289,#151290,#151291,#151292,#151293,#151294,
#151295,#151296,#151297,#151298,#151299,#151300,#151301,#151302,#151303,
#151304,#151305,#151306,#151307,#151308,#151309,#151310,#151311,#151312,
#151313,#151314,#151315,#151316,#151317,#151318,#151319,#151320,#151321,
#151322,#151323,#151324,#151325,#151326,#151327,#151328,#151329,#151330,
#151331,#151332,#151333,#151334,#151335,#151336,#151337,#151338,#151339,
#151340,#151341,#151342,#151343,#151344,#151345,#151346,#151347,#151348,
#151349,#151350,#151351,#151352,#151353,#151354,#151355,#151356,#151357,
#151358,#151359,#151360,#151361,#151362,#151363,#151364,#151365,#151366,
#151367,#151368,#151369,#151370,#151371,#151372,#151373,#151374,#151375,
#151376,#151377,#151378,#151379,#151380,#151381,#151382,#151383,#151384,
#151385,#151386,#151387,#151388,#151389,#151390,#151391,#151392,#151393,
#151394,#151395),.UNSPECIFIED.,.F.,.F.,(4,3,3,3,3,3,3,3,3,3,3,3,3,3,3,3,
3,3,3,3,3,3,3,3,3,3,3,3,3,3,3,3,3,3,3,3,3,3,3,3,3,4),(28.2743338823082,
28.3823371513587,28.4809354104368,28.5793933287022,28.6796158627795,28.7778955584748,
28.8761422761379,28.9743854982056,29.0760825239843,29.1744670761058,29.2778203387132,
29.3811736013206,29.4797717427275,29.5782295425788,29.6784521061668,29.7767316825037,
29.8749782807199,29.9732213834117,30.0749185503794,30.1733029845339,30.2766565179082,
30.3800100512825,30.4786081309532,30.5770658676386,30.6772884468394,30.7755679569466,
30.8738144879313,30.9720575224759,31.073754767168,31.1721391315728,31.2754928164085,
31.3788465012443,31.47744774742,31.5759078068145,31.6742504133382,31.772528758262,
31.8707723652669,31.969010716985,32.0673303014884,32.1656922455267,32.264202766454,
32.3314302948912),.UNSPECIFIED.);
#1597=B_SPLINE_CURVE_WITH_KNOTS('',3,(#151401,#151402,#151403,#151404,#151405,
#151406,#151407,#151408,#151409,#151410,#151411,#151412,#151413,#151414,
#151415,#151416,#151417,#151418,#151419,#151420,#151421,#151422,#151423,
#151424,#151425,#151426,#151427,#151428,#151429,#151430,#151431,#151432,
#151433,#151434,#151435,#151436,#151437,#151438,#151439,#151440,#151441,
#151442,#151443,#151444,#151445,#151446,#151447,#151448,#151449,#151450,
#151451,#151452,#151453,#151454,#151455,#151456,#151457,#151458,#151459,
#151460,#151461,#151462,#151463,#151464,#151465,#151466,#151467,#151468,
#151469,#151470,#151471,#151472,#151473,#151474,#151475,#151476,#151477,
#151478,#151479,#151480,#151481,#151482,#151483,#151484,#151485,#151486,
#151487,#151488,#151489,#151490,#151491,#151492,#151493,#151494,#151495,
#151496,#151497,#151498,#151499,#151500,#151501,#151502,#151503,#151504,
#151505,#151506,#151507,#151508,#151509,#151510,#151511,#151512,#151513,
#151514,#151515,#151516,#151517,#151518,#151519,#151520,#151521,#151522,
#151523,#151524),.UNSPECIFIED.,.F.,.F.,(4,3,3,3,3,3,3,3,3,3,3,3,3,3,3,3,
3,3,3,3,3,3,3,3,3,3,3,3,3,3,3,3,3,3,3,3,3,3,3,3,3,4),(34.5575191897594,
34.6782345503652,34.8009387396128,34.8401625836495,34.938760709128,35.0372184923859,
35.1374410600391,35.2357206182604,35.3339671978303,35.432210281368,35.5339074694289,
35.6322918833488,35.7356454584801,35.8389990336114,35.9375971585483,36.0360549412584,
36.1362775090477,36.2345570667101,36.3328036457183,36.431046728692,36.5327439174123,
36.6311283307686,36.7344819071709,36.8378354835733,36.9364336084867,37.0348913911713,
37.1351139589668,37.2333935165991,37.3316400955754,37.4298831785158,37.5315803672706,
37.6299647805896,37.7333183570624,37.8366719335352,37.9352415778389,38.0336830992457,
38.1320262041044,38.2303004962127,38.3285627936486,38.4268127465031,38.5251372404174,
38.6142676068576),.UNSPECIFIED.);
#1598=B_SPLINE_CURVE_WITH_KNOTS('',3,(#151525,#151526,#151527,#151528,#151529,
#151530,#151531,#151532,#151533,#151534,#151535,#151536,#151537,#151538,
#151539,#151540,#151541,#151542,#151543,#151544,#151545,#151546,#151547,
#151548,#151549,#151550,#151551,#151552,#151553,#151554,#151555,#151556,
#151557,#151558,#151559,#151560,#151561,#151562,#151563,#151564,#151565,
#151566,#151567,#151568,#151569,#151570,#151571,#151572,#151573,#151574,
#151575,#151576,#151577,#151578,#151579,#151580,#151581,#151582,#151583,
#151584,#151585,#151586,#151587,#151588,#151589,#151590,#151591,#151592,
#151593,#151594,#151595,#151596,#151597),.UNSPECIFIED.,.F.,.F.,(4,3,3,3,
3,3,3,3,3,3,3,3,3,3,3,3,3,3,3,3,3,3,3,3,4),(32.331714743168,32.4299572228888,
32.533090338098,32.6314722618068,32.7299237843655,32.8285286363519,32.8424896837258,
32.941087808515,33.039545591083,33.1397681589086,33.2380477164422,33.3362942953269,
33.434537378183,33.5362345670592,33.634618980313,33.7379725570004,33.8413261336877,
33.9390973941506,34.0367388270547,34.1342810926888,34.2317547370042,34.3292101035739,
34.4266554953284,34.5241539309046,34.5575191894878),.UNSPECIFIED.);
#1599=B_SPLINE_CURVE_WITH_KNOTS('',3,(#151599,#151600,#151601,#151602,#151603,
#151604,#151605,#151606,#151607,#151608,#151609,#151610,#151611,#151612,
#151613,#151614,#151615,#151616,#151617,#151618,#151619,#151620,#151621,
#151622,#151623,#151624,#151625,#151626,#151627,#151628,#151629,#151630,
#151631,#151632,#151633,#151634,#151635,#151636,#151637,#151638,#151639,
#151640,#151641,#151642,#151643,#151644,#151645,#151646,#151647,#151648,
#151649,#151650,#151651,#151652,#151653,#151654,#151655,#151656,#151657,
#151658,#151659,#151660,#151661,#151662,#151663,#151664,#151665,#151666,
#151667,#151668),.UNSPECIFIED.,.F.,.F.,(4,3,3,3,3,3,3,3,3,3,3,3,3,3,3,3,
3,3,3,3,3,3,3,4),(32.3314302948912,32.3776829512062,32.4762810765929,32.5747388598192,
32.6749614274878,32.7732409858268,32.8714875655702,32.9697306493372,33.0714278372949,
33.169812251582,33.273165826375,33.3765194011681,33.4751175202855,33.5735752970726,
33.6737978663298,33.7720774178574,33.8703239906649,33.9685670673804,34.0702642633178,
34.1686486703349,34.2720022607324,34.37535585113,34.5238559810743,34.5575191894878),
 .UNSPECIFIED.);
#1600=B_SPLINE_CURVE_WITH_KNOTS('',3,(#151669,#151670,#151671,#151672,#151673,
#151674,#151675,#151676),.UNSPECIFIED.,.F.,.F.,(4,1,1,1,1,4),(34.5575241466493,
35.3741923010918,36.3730287510537,37.3718652010156,38.3707016509774,38.6157831097427),
 .UNSPECIFIED.);
#1601=B_SPLINE_CURVE_WITH_KNOTS('',3,(#151682,#151683,#151684,#151685,#151686,
#151687,#151688,#151689,#151690,#151691,#151692,#151693,#151694,#151695,
#151696,#151697,#151698,#151699,#151700,#151701,#151702,#151703,#151704,
#151705,#151706,#151707,#151708,#151709,#151710,#151711,#151712,#151713,
#151714,#151715,#151716,#151717,#151718,#151719,#151720,#151721,#151722,
#151723,#151724,#151725,#151726,#151727,#151728,#151729,#151730,#151731,
#151732,#151733,#151734,#151735,#151736,#151737,#151738,#151739,#151740,
#151741,#151742,#151743,#151744,#151745,#151746,#151747,#151748,#151749,
#151750,#151751,#151752,#151753,#151754,#151755,#151756,#151757,#151758,
#151759,#151760,#151761,#151762,#151763,#151764,#151765,#151766,#151767,
#151768,#151769,#151770,#151771,#151772,#151773,#151774,#151775,#151776,
#151777,#151778,#151779,#151780,#151781,#151782,#151783,#151784,#151785,
#151786,#151787,#151788,#151789,#151790,#151791,#151792,#151793,#151794,
#151795,#151796,#151797,#151798,#151799,#151800,#151801,#151802,#151803,
#151804,#151805),.UNSPECIFIED.,.F.,.F.,(4,3,3,3,3,3,3,3,3,3,3,3,3,3,3,3,
3,3,3,3,3,3,3,3,3,3,3,3,3,3,3,3,3,3,3,3,3,3,3,3,3,4),(40.8407044969197,
40.9391705387198,41.037496428004,41.1368115911763,41.2349607512892,41.3330774110127,
41.4311912274061,41.5313978539003,41.6296531901072,41.730835461745,41.8320177333827,
41.9306158583838,42.029073641158,42.1292962089313,42.2275757666567,42.3258223457274,
42.4240654287631,42.5257626174084,42.6241470308245,42.7275006070845,42.8308541833445,
42.9294523083471,43.0279100911227,43.1281326588956,43.2264122166225,43.3246587956947,
43.4229018787317,43.5245990673754,43.6229834807929,43.7263370570496,43.8296906333064,
43.9282887583115,44.0267465410895,44.1269691088619,44.2252486665914,44.3234952456661,
44.421738328706,44.5234355173466,44.6218199307668,44.7251735070175,44.8285270832683,
44.898397912177),.UNSPECIFIED.);
#1602=B_SPLINE_CURVE_WITH_KNOTS('',3,(#151806,#151807,#151808,#151809,#151810,
#151811,#151812,#151813,#151814,#151815,#151816,#151817,#151818,#151819,
#151820,#151821,#151822,#151823,#151824,#151825,#151826,#151827,#151828,
#151829,#151830,#151831,#151832,#151833,#151834,#151835,#151836,#151837,
#151838,#151839,#151840,#151841,#151842,#151843,#151844,#151845,#151846,
#151847,#151848,#151849,#151850,#151851,#151852,#151853,#151854,#151855,
#151856,#151857,#151858,#151859,#151860,#151861,#151862,#151863,#151864,
#151865,#151866,#151867,#151868,#151869,#151870,#151871,#151872,#151873,
#151874,#151875,#151876,#151877,#151878),.UNSPECIFIED.,.F.,.F.,(4,3,3,3,
3,3,3,3,3,3,3,3,3,3,3,3,3,3,3,3,3,3,3,3,4),(38.6142676068576,38.7127106610344,
38.8113098761237,38.835508383497,38.9341065084864,39.0325642912489,39.1327868590251,
39.2310664167389,39.3293129957979,39.4275560788221,39.5292532674813,39.627637680886,
39.7309912571724,39.8343448334589,39.9329429584521,40.0314007412181,40.1316233089934,
40.2299028667104,40.3281494457725,40.4263925287995,40.5280897174548,40.6264741308619,
40.7298277071414,40.8331812834208,40.8407044966674),.UNSPECIFIED.);
#1603=B_SPLINE_CURVE_WITH_KNOTS('',3,(#151880,#151881,#151882,#151883,#151884,
#151885),.UNSPECIFIED.,.F.,.F.,(4,1,1,4),(38.6157831097427,39.3695381009393,
40.3683745509012,40.8407024148877),.UNSPECIFIED.);
#1604=B_SPLINE_CURVE_WITH_KNOTS('',3,(#151886,#151887,#151888,#151889,#151890,
#151891,#151892,#151893,#151894,#151895,#151896,#151897,#151898,#151899,
#151900,#151901,#151902,#151903,#151904,#151905,#151906,#151907,#151908,
#151909,#151910,#151911,#151912,#151913,#151914,#151915,#151916,#151917,
#151918,#151919,#151920,#151921,#151922,#151923,#151924,#151925,#151926,
#151927,#151928,#151929,#151930,#151931,#151932,#151933,#151934,#151935,
#151936,#151937,#151938,#151939,#151940,#151941,#151942,#151943,#151944,
#151945,#151946,#151947,#151948,#151949,#151950,#151951,#151952,#151953,
#151954,#151955,#151956,#151957,#151958,#151959,#151960,#151961,#151962,
#151963,#151964,#151965,#151966,#151967,#151968,#151969,#151970,#151971,
#151972,#151973,#151974,#151975,#151976,#151977,#151978,#151979,#151980,
#151981,#151982,#151983,#151984,#151985,#151986,#151987,#151988,#151989,
#151990,#151991,#151992,#151993,#151994,#151995,#151996,#151997,#151998,
#151999,#152000,#152001,#152002,#152003,#152004,#152005,#152006,#152007,
#152008,#152009,#152010,#152011,#152012),.UNSPECIFIED.,.F.,.F.,(4,3,3,3,
3,3,3,3,3,3,3,3,3,3,3,3,3,3,3,3,3,3,3,3,3,3,3,3,3,3,3,3,3,3,3,3,3,3,3,3,
3,3,4),(40.8407044966674,40.9425310419933,41.0487010317108,41.1508691915798,
41.2531658485548,41.3556785603237,41.3672110008631,41.4658091258525,41.5642669086149,
41.6644894763911,41.7627690341048,41.8610156131638,41.959258696188,42.0609558848473,
42.1593402982519,42.2626938745384,42.3660474508249,42.4646455758181,42.5631033585842,
42.6633259263595,42.7616054840764,42.8598520631386,42.9580951461657,43.0597923348209,
43.1581767482281,43.2615303245074,43.3648839007868,43.4634820258002,43.5619398085866,
43.6621623763569,43.7604419340952,43.858688513179,43.956931596228,44.0586287848581,
44.1570131982874,44.260366774518,44.3637203507487,44.4623140220593,44.5607732131683,
44.6591152246882,44.7573894748901,44.8556332863445,44.8979422484848),
 .UNSPECIFIED.);
#1605=B_SPLINE_CURVE_WITH_KNOTS('',3,(#152018,#152019,#152020,#152021,#152022,
#152023,#152024,#152025),.UNSPECIFIED.,.F.,.F.,(4,1,1,1,1,4),(47.123889803847,
47.8250364331539,48.8238728831158,49.8227093330777,50.8215457830395,51.1819113477222),
 .UNSPECIFIED.);
#1606=B_SPLINE_CURVE_WITH_KNOTS('',3,(#152026,#152027,#152028,#152029,#152030,
#152031,#152032,#152033,#152034,#152035,#152036,#152037,#152038,#152039,
#152040,#152041,#152042,#152043,#152044,#152045,#152046,#152047,#152048,
#152049,#152050,#152051,#152052,#152053,#152054,#152055,#152056,#152057,
#152058,#152059,#152060,#152061,#152062,#152063,#152064,#152065,#152066,
#152067,#152068,#152069,#152070,#152071,#152072,#152073,#152074,#152075,
#152076,#152077,#152078,#152079,#152080,#152081,#152082,#152083,#152084,
#152085,#152086,#152087,#152088,#152089,#152090,#152091,#152092,#152093,
#152094,#152095),.UNSPECIFIED.,.F.,.F.,(4,3,3,3,3,3,3,3,3,3,3,3,3,3,3,3,
3,3,3,3,3,3,3,4),(44.898397912177,44.996893211109,45.0952714368175,45.1935672422509,
45.2918209058777,45.3900619196009,45.4883197545766,45.5866858960032,45.6851136444438,
45.7837031196575,45.8273635332302,45.9259616582338,46.0244194410105,46.1246420087832,
46.2229215665111,46.3211681455844,46.4194112286225,46.5211084172649,46.6194928306835,
46.7228464069377,46.826199983192,46.9466622822341,47.0654828012636,47.1238896269672),
 .UNSPECIFIED.);
#1607=B_SPLINE_CURVE_WITH_KNOTS('',3,(#152097,#152098,#152099,#152100,#152101,
#152102,#152103,#152104,#152105,#152106,#152107,#152108,#152109,#152110,
#152111,#152112,#152113,#152114,#152115,#152116,#152117,#152118,#152119,
#152120,#152121,#152122,#152123,#152124,#152125,#152126,#152127,#152128,
#152129,#152130,#152131,#152132,#152133,#152134,#152135,#152136,#152137,
#152138,#152139,#152140,#152141,#152142,#152143,#152144,#152145,#152146,
#152147,#152148,#152149,#152150,#152151,#152152,#152153,#152154,#152155,
#152156,#152157,#152158,#152159,#152160,#152161,#152162,#152163,#152164,
#152165,#152166),.UNSPECIFIED.,.F.,.F.,(4,3,3,3,3,3,3,3,3,3,3,3,3,3,3,3,
3,3,3,3,3,3,3,4),(44.8979422484848,44.9961924492798,45.0945461787255,45.1929541521146,
45.2915320845352,45.3625568007106,45.4611549257132,45.5596127084889,45.6598352762619,
45.7581148339888,45.856361413061,45.9546044960982,46.0563016847417,46.1546860981591,
46.2580396744158,46.3613932506724,46.4587199838046,46.5559210250952,46.6530274701203,
46.7500702965179,46.8471124553621,46.9441490048064,47.0412721236584,47.123889803847),
 .UNSPECIFIED.);
#1608=B_SPLINE_CURVE_WITH_KNOTS('',3,(#152167,#152168,#152169,#152170,#152171,
#152172,#152173,#152174),.UNSPECIFIED.,.F.,.F.,(4,1,1,1,1,4),(47.1238901033263,
47.3602297006343,48.3590661505962,49.3579026005581,50.3567390505199,51.1803881393169),
 .UNSPECIFIED.);
#1609=B_SPLINE_CURVE_WITH_KNOTS('',3,(#152180,#152181,#152182,#152183,#152184,
#152185,#152186,#152187,#152188,#152189,#152190,#152191,#152192,#152193,
#152194,#152195,#152196,#152197,#152198,#152199,#152200,#152201,#152202,
#152203,#152204,#152205,#152206,#152207,#152208,#152209,#152210,#152211,
#152212,#152213,#152214,#152215,#152216,#152217,#152218,#152219,#152220,
#152221,#152222,#152223,#152224,#152225,#152226,#152227,#152228,#152229,
#152230,#152231,#152232,#152233,#152234,#152235,#152236,#152237,#152238,
#152239,#152240,#152241,#152242,#152243,#152244,#152245,#152246,#152247,
#152248,#152249,#152250,#152251,#152252,#152253,#152254,#152255,#152256,
#152257,#152258,#152259,#152260,#152261,#152262,#152263,#152264,#152265,
#152266,#152267,#152268,#152269,#152270,#152271,#152272,#152273,#152274,
#152275,#152276,#152277,#152278,#152279,#152280,#152281,#152282,#152283,
#152284,#152285,#152286,#152287,#152288,#152289,#152290,#152291,#152292,
#152293,#152294,#152295,#152296,#152297,#152298,#152299,#152300,#152301,
#152302,#152303),.UNSPECIFIED.,.F.,.F.,(4,3,3,3,3,3,3,3,3,3,3,3,3,3,3,3,
3,3,3,3,3,3,3,3,3,3,3,3,3,3,3,3,3,3,3,3,3,3,3,3,3,4),(53.4070755243615,
53.5149520672712,53.6231638610662,53.7318758460164,53.8180551329252,53.9166532579289,
54.0151110407057,54.1153336084784,54.2136131662065,54.3118597452799,54.4101028283183,
54.5118000169605,54.6101844303793,54.7135380066332,54.816891582887,54.9154897078907,
55.0139474906675,55.1141700584402,55.2124496161683,55.3106961952417,55.4089392782802,
55.5106364669224,55.6090208803412,55.7123744565951,55.8157280328489,55.9143261578526,
56.0127839406294,56.113006508402,56.2112860661302,56.3095326452036,56.4077757282421,
56.5094729168843,56.6078573303031,56.7112109065569,56.8145644828108,56.9131452274625,
57.0115945031705,57.1099420320622,57.2082227592595,57.3064633876106,57.4047205556631,
57.4639959186668),.UNSPECIFIED.);
#1610=B_SPLINE_CURVE_WITH_KNOTS('',3,(#152304,#152305,#152306,#152307,#152308,
#152309),.UNSPECIFIED.,.F.,.F.,(4,1,1,4),(51.1819113477222,51.8203822330014,
52.8192186829633,53.4070751110266),.UNSPECIFIED.);
#1611=B_SPLINE_CURVE_WITH_KNOTS('',3,(#152311,#152312,#152313,#152314,#152315,
#152316,#152317),.UNSPECIFIED.,.F.,.F.,(4,1,1,1,4),(51.1803881393169,51.3555755004818,
52.3544119504437,53.3532484004056,53.4070751110266),.UNSPECIFIED.);
#1612=B_SPLINE_CURVE_WITH_KNOTS('',3,(#152318,#152319,#152320,#152321,#152322,
#152323,#152324,#152325,#152326,#152327,#152328,#152329,#152330,#152331,
#152332,#152333,#152334,#152335,#152336,#152337,#152338,#152339,#152340,
#152341,#152342,#152343,#152344,#152345,#152346,#152347,#152348,#152349,
#152350,#152351,#152352,#152353,#152354,#152355,#152356,#152357,#152358,
#152359,#152360,#152361,#152362,#152363,#152364,#152365,#152366,#152367,
#152368,#152369,#152370,#152371,#152372,#152373,#152374,#152375,#152376,
#152377,#152378,#152379,#152380,#152381,#152382,#152383,#152384,#152385,
#152386,#152387,#152388,#152389,#152390,#152391,#152392,#152393,#152394,
#152395,#152396,#152397,#152398,#152399,#152400,#152401,#152402,#152403,
#152404,#152405,#152406,#152407,#152408,#152409,#152410,#152411,#152412,
#152413,#152414,#152415,#152416,#152417,#152418,#152419,#152420,#152421,
#152422,#152423,#152424,#152425,#152426,#152427,#152428,#152429,#152430,
#152431,#152432,#152433,#152434,#152435,#152436,#152437,#152438,#152439,
#152440,#152441,#152442,#152443,#152444),.UNSPECIFIED.,.F.,.F.,(4,3,3,3,
3,3,3,3,3,3,3,3,3,3,3,3,3,3,3,3,3,3,3,3,3,3,3,3,3,3,3,3,3,3,3,3,3,3,3,3,
3,3,4),(53.4070751110266,53.5048543854907,53.6024983707769,53.7000367768843,
53.7975186210124,53.8949743677959,53.9924344477701,54.0899931990353,54.1876041339863,
54.2853815723758,54.3520848503674,54.4506829753712,54.549140758148,54.6493633259207,
54.7476428836488,54.8458894627222,54.9441325457608,55.0458297344029,55.1442141478217,
55.2475677240755,55.3509213003293,55.449519425333,55.5479772081097,55.6481997758824,
55.7464793336105,55.8447259126839,55.9429689957224,56.0446661843646,56.1430505977834,
56.2464041740373,56.3497577502912,56.4483558752948,56.5468136580714,56.6470362258441,
56.7453157835723,56.8435623626456,56.9418054456843,57.0435026343265,57.1418870477453,
57.2452406239992,57.3485942002531,57.4471969426278,57.4649113323326),
 .UNSPECIFIED.);
#1613=B_SPLINE_CURVE_WITH_KNOTS('',3,(#152450,#152451,#152452,#152453,#152454,
#152455,#152456,#152457),.UNSPECIFIED.,.F.,.F.,(4,1,1,1,1,4),(59.6902604182062,
59.8110738326964,60.8099102826583,61.8087467326202,62.807583182582,63.7472417658755),
 .UNSPECIFIED.);
#1614=B_SPLINE_CURVE_WITH_KNOTS('',3,(#152458,#152459,#152460,#152461,#152462,
#152463,#152464,#152465,#152466,#152467,#152468,#152469,#152470,#152471,
#152472,#152473,#152474,#152475,#152476,#152477,#152478,#152479,#152480,
#152481,#152482,#152483,#152484,#152485,#152486,#152487,#152488,#152489,
#152490,#152491,#152492,#152493,#152494,#152495,#152496,#152497,#152498,
#152499,#152500,#152501,#152502,#152503,#152504,#152505,#152506,#152507,
#152508,#152509,#152510,#152511,#152512,#152513,#152514,#152515,#152516,
#152517,#152518,#152519,#152520,#152521,#152522,#152523,#152524,#152525,
#152526,#152527),.UNSPECIFIED.,.F.,.F.,(4,3,3,3,3,3,3,3,3,3,3,3,3,3,3,3,
3,3,3,3,3,3,3,4),(57.4639959186668,57.5623571123803,57.6607771204479,57.7593619216273,
57.8134009327727,57.9119990577764,58.010456840553,58.1106794083257,58.2089589660538,
58.3072055451272,58.4054486281658,58.507145816808,58.6055302302267,58.7088838064806,
58.8122373827345,58.9094791608007,59.0070768179764,59.1040671063403,59.2009981633323,
59.2979009849174,59.3959908432396,59.4929780422902,59.5916192302482,59.6902604182062),
 .UNSPECIFIED.);
#1615=B_SPLINE_CURVE_WITH_KNOTS('',3,(#152529,#152530,#152531,#152532,#152533,
#152534,#152535,#152536,#152537,#152538,#152539,#152540,#152541,#152542,
#152543,#152544,#152545,#152546,#152547,#152548,#152549,#152550,#152551,
#152552,#152553,#152554,#152555,#152556,#152557,#152558,#152559,#152560,
#152561,#152562,#152563,#152564,#152565,#152566,#152567,#152568,#152569,
#152570,#152571,#152572,#152573,#152574,#152575,#152576,#152577,#152578,
#152579,#152580,#152581,#152582,#152583,#152584,#152585,#152586,#152587,
#152588,#152589,#152590,#152591,#152592,#152593,#152594,#152595),
 .UNSPECIFIED.,.F.,.F.,(4,3,3,3,3,3,3,3,3,3,3,3,3,3,3,3,3,3,3,3,3,3,4),
(57.4649113323326,57.5633473588617,57.6616773741524,57.7599496392934,57.8581936678956,
57.9564389387784,58.0547832309801,58.1531751315162,58.2517448177315,58.3474306502149,
58.4460287752186,58.5444865579952,58.6447091257679,58.742988683496,58.8412352625694,
58.9394783456079,59.0411755342501,59.139559947669,59.2429135239229,59.3462671001768,
59.4608829140306,59.5755716660049,59.6902604179793),.UNSPECIFIED.);
#1616=B_SPLINE_CURVE_WITH_KNOTS('',3,(#152596,#152597,#152598,#152599,#152600,
#152601,#152602,#152603,#152604,#152605,#152606,#152607,#152608,#152609,
#152610,#152611,#152612,#152613,#152614,#152615,#152616,#152617,#152618,
#152619,#152620,#152621,#152622,#152623,#152624,#152625,#152626,#152627,
#152628,#152629,#152630,#152631,#152632,#152633,#152634,#152635,#152636,
#152637,#152638,#152639,#152640,#152641,#152642,#152643,#152644,#152645,
#152646,#152647,#152648,#152649,#152650,#152651,#152652,#152653,#152654,
#152655,#152656,#152657,#152658,#152659,#152660,#152661,#152662,#152663,
#152664,#152665,#152666,#152667,#152668,#152669,#152670,#152671,#152672,
#152673,#152674,#152675,#152676,#152677,#152678,#152679,#152680,#152681,
#152682,#152683,#152684,#152685,#152686,#152687,#152688,#152689,#152690,
#152691,#152692,#152693,#152694,#152695,#152696,#152697,#152698,#152699,
#152700,#152701,#152702,#152703,#152704,#152705,#152706,#152707,#152708,
#152709,#152710,#152711,#152712,#152713,#152714,#152715,#152716,#152717,
#152718,#152719),.UNSPECIFIED.,.F.,.F.,(4,3,3,3,3,3,3,3,3,3,3,3,3,3,3,3,
3,3,3,3,3,3,3,3,3,3,3,3,3,3,3,3,3,3,3,3,3,3,3,3,3,4),(59.6902604182062,
59.788634173056,59.8869985815969,59.9853827919993,60.0838846667642,60.1824499292134,
60.2811933482972,60.3451035501387,60.4437016751424,60.5421594579191,60.6423820256918,
60.7406615834199,60.8389081624934,60.937151245532,61.0388484341741,61.1372328475929,
61.2405864238468,61.3439400001006,61.4425381251044,61.5409959078813,61.641218475654,
61.7394980333821,61.8377446124555,61.935987695494,62.0376848841361,62.1360692975549,
62.2394228738086,62.3427764500624,62.4413745750661,62.5398323578429,62.6400549256156,
62.7383344833437,62.836581062417,62.9348241454556,63.0365213340978,63.1349057475167,
63.2382593237705,63.3416129000243,63.4431811117946,63.5416227526594,63.6447542498824,
63.7478857471053),.UNSPECIFIED.);
#1617=B_SPLINE_CURVE_WITH_KNOTS('',3,(#152725,#152726,#152727,#152728,#152729,
#152730,#152731,#152732,#152733,#152734,#152735,#152736,#152737,#152738,
#152739,#152740,#152741,#152742,#152743,#152744,#152745,#152746,#152747,
#152748,#152749,#152750,#152751,#152752,#152753,#152754,#152755,#152756,
#152757,#152758,#152759,#152760,#152761,#152762,#152763,#152764,#152765,
#152766,#152767,#152768,#152769,#152770,#152771,#152772,#152773,#152774,
#152775,#152776,#152777,#152778,#152779,#152780,#152781,#152782,#152783,
#152784,#152785,#152786,#152787,#152788,#152789,#152790,#152791,#152792,
#152793,#152794,#152795,#152796,#152797,#152798,#152799,#152800,#152801,
#152802,#152803,#152804,#152805,#152806,#152807,#152808,#152809,#152810,
#152811,#152812,#152813,#152814,#152815,#152816,#152817,#152818,#152819,
#152820,#152821,#152822,#152823,#152824,#152825,#152826,#152827,#152828,
#152829,#152830,#152831,#152832,#152833,#152834,#152835,#152836,#152837,
#152838,#152839,#152840,#152841,#152842,#152843,#152844,#152845,#152846,
#152847,#152848,#152849,#152850,#152851),.UNSPECIFIED.,.F.,.F.,(4,3,3,3,
3,3,3,3,3,3,3,3,3,3,3,3,3,3,3,3,3,3,3,3,3,3,3,3,3,3,3,3,3,3,3,3,3,3,3,3,
3,3,4),(65.9734457253857,66.0704340596178,66.1673127975358,66.264132888756,
66.360925426791,66.4577214670338,66.5546134226801,66.6515579893416,66.7486626585399,
66.8029289824295,66.9015271074332,66.99998489021,67.1002074579826,67.1984870157108,
67.2967335947843,67.3949766778228,67.4966738664649,67.5950582798837,67.6984118561376,
67.8017654323914,67.900363557395,67.9988213401718,68.0990439079444,68.1973234656726,
68.295570044746,68.3938131277846,68.4955103164268,68.5938947298455,68.6972483060994,
68.8006018823533,68.8992000073569,68.9976577901338,69.0978803579064,69.1961599156346,
69.294406494708,69.3926495777466,69.4943467663888,69.5927311798075,69.6960847560613,
69.7994383323151,69.8980412657884,69.9964918402605,70.0313848974635),
 .UNSPECIFIED.);
#1618=B_SPLINE_CURVE_WITH_KNOTS('',3,(#152852,#152853,#152854,#152855,#152856,
#152857,#152858),.UNSPECIFIED.,.F.,.F.,(4,1,1,1,4),(63.7472417658755,63.8064196325439,
64.8052560825058,65.8040925324676,65.9734457253857),.UNSPECIFIED.);
#1619=B_SPLINE_CURVE_WITH_KNOTS('',3,(#152860,#152861,#152862,#152863,#152864,
#152865,#152866,#152867,#152868,#152869,#152870,#152871,#152872,#152873,
#152874,#152875,#152876,#152877,#152878,#152879,#152880,#152881,#152882,
#152883,#152884,#152885,#152886,#152887,#152888,#152889,#152890,#152891,
#152892,#152893,#152894,#152895,#152896,#152897,#152898,#152899,#152900,
#152901,#152902,#152903,#152904,#152905,#152906,#152907,#152908,#152909,
#152910,#152911,#152912,#152913,#152914,#152915,#152916,#152917,#152918,
#152919,#152920,#152921,#152922,#152923,#152924,#152925,#152926,#152927,
#152928,#152929),.UNSPECIFIED.,.F.,.F.,(4,3,3,3,3,3,3,3,3,3,3,3,3,3,3,3,
3,3,3,3,3,3,3,4),(63.7478857471053,63.8461305131556,63.9443749970032,64.0433935852489,
64.1417827849983,64.2411160674923,64.3404493499862,64.4390474749898,64.5375052577667,
64.6377278255393,64.7360073832674,64.8342539623408,64.9324970453792,65.0341942340214,
65.1325786474401,65.2359322236941,65.3392857999481,65.4384637976084,65.5374980774502,
65.6364173808603,65.7352455972603,65.8340208922133,65.9327849002203,65.9734457253857),
 .UNSPECIFIED.);
#1620=B_SPLINE_CURVE_WITH_KNOTS('',3,(#152930,#152931,#152932,#152933,#152934,
#152935,#152936,#152937,#152938,#152939,#152940,#152941,#152942,#152943,
#152944,#152945,#152946,#152947,#152948,#152949,#152950,#152951,#152952,
#152953,#152954,#152955,#152956,#152957,#152958,#152959,#152960,#152961,
#152962,#152963,#152964,#152965,#152966,#152967,#152968,#152969,#152970,
#152971,#152972,#152973,#152974,#152975,#152976,#152977,#152978,#152979,
#152980,#152981,#152982,#152983,#152984,#152985,#152986,#152987,#152988,
#152989,#152990,#152991,#152992,#152993,#152994,#152995,#152996,#152997,
#152998,#152999,#153000,#153001,#153002,#153003,#153004,#153005,#153006,
#153007,#153008,#153009,#153010,#153011,#153012,#153013,#153014,#153015,
#153016,#153017,#153018,#153019,#153020,#153021,#153022,#153023,#153024,
#153025,#153026,#153027,#153028,#153029,#153030,#153031,#153032,#153033,
#153034,#153035,#153036,#153037,#153038,#153039,#153040,#153041,#153042,
#153043,#153044,#153045,#153046,#153047,#153048,#153049,#153050,#153051,
#153052,#153053),.UNSPECIFIED.,.F.,.F.,(4,3,3,3,3,3,3,3,3,3,3,3,3,3,3,3,
3,3,3,3,3,3,3,3,3,3,3,3,3,3,3,3,3,3,3,3,3,3,3,3,3,4),(65.9734457256204,
66.084879805074,66.1968635637049,66.3094957826842,66.3381222499099,66.4367203749136,
66.5351781576905,66.6354007254632,66.7336802831913,66.8319268622647,66.9301699453032,
67.0318671339454,67.1302515473642,67.233605123618,67.3369586998718,67.4355568248755,
67.5340146076523,67.634237175425,67.7325167331532,67.8307633122266,67.9290063952651,
68.0307035839072,68.1290879973261,68.2324415735799,68.3357951498337,68.4343932748374,
68.5328510576142,68.6330736253868,68.731353183115,68.8295997621883,68.9278428452268,
69.029540033869,69.1279244472878,69.2312780235417,69.3346315997956,69.433207943652,
69.5316540255099,69.6299995615715,69.7300683883787,69.8283147588378,69.9292948138189,
70.0302748688001),.UNSPECIFIED.);
#1621=B_SPLINE_CURVE_WITH_KNOTS('',3,(#153059,#153060,#153061,#153062,#153063,
#153064,#153065,#153066),.UNSPECIFIED.,.F.,.F.,(4,1,1,1,1,4),(72.2566310325654,
72.7959476822008,73.7947841321626,74.7936205821245,75.7924570320864,76.3138574014144),
 .UNSPECIFIED.);
#1622=B_SPLINE_CURVE_WITH_KNOTS('',3,(#153067,#153068,#153069,#153070,#153071,
#153072,#153073,#153074,#153075,#153076,#153077,#153078,#153079,#153080,
#153081,#153082,#153083,#153084,#153085,#153086,#153087,#153088,#153089,
#153090,#153091,#153092,#153093,#153094,#153095,#153096,#153097,#153098,
#153099,#153100,#153101,#153102,#153103,#153104,#153105,#153106,#153107,
#153108,#153109,#153110,#153111,#153112,#153113,#153114,#153115,#153116,
#153117,#153118,#153119,#153120,#153121,#153122,#153123,#153124,#153125,
#153126,#153127,#153128,#153129,#153130,#153131,#153132,#153133,#153134,
#153135,#153136),.UNSPECIFIED.,.F.,.F.,(4,3,3,3,3,3,3,3,3,3,3,3,3,3,3,3,
3,3,3,3,3,3,3,4),(70.0313848974635,70.1297026871758,70.2279678893552,70.3262100096092,
70.4244585234034,70.5228092220642,70.6212121566704,70.7197873779156,70.798274782277,
70.8968729072808,70.9953306900579,71.0955532578305,71.1938328155586,71.2920793946318,
71.3903224776704,71.4920196663125,71.5904040797314,71.6937576559851,71.7971112322389,
71.9028340905518,72.0081993817383,72.1133399321502,72.2181701837247,72.2566308185806),
 .UNSPECIFIED.);
#1623=B_SPLINE_CURVE_WITH_KNOTS('',3,(#153138,#153139,#153140,#153141,#153142,
#153143,#153144,#153145,#153146,#153147,#153148,#153149,#153150,#153151,
#153152,#153153,#153154,#153155,#153156,#153157,#153158,#153159,#153160,
#153161,#153162,#153163,#153164,#153165,#153166,#153167,#153168,#153169,
#153170,#153171,#153172,#153173,#153174,#153175,#153176,#153177,#153178,
#153179,#153180,#153181,#153182,#153183,#153184,#153185,#153186,#153187,
#153188,#153189,#153190,#153191,#153192,#153193,#153194,#153195,#153196,
#153197,#153198,#153199,#153200,#153201,#153202,#153203,#153204,#153205,
#153206,#153207),.UNSPECIFIED.,.F.,.F.,(4,3,3,3,3,3,3,3,3,3,3,3,3,3,3,3,
3,3,3,3,3,3,3,4),(70.0302748688001,70.1286603970033,70.2310642233803,70.3334680497574,
70.4320661747611,70.5305239575378,70.6307465253105,70.7290260830386,70.827272662112,
70.9255157451506,71.0272129337928,71.1255973472115,71.2289509234654,71.3323044997193,
71.4298807240689,71.5273176349422,71.6246428433671,71.7219081150621,71.8191441424517,
71.9163815796695,72.013708783522,72.1110862397604,72.2086145464311,72.2566310325654),
 .UNSPECIFIED.);
#1624=B_SPLINE_CURVE_WITH_KNOTS('',3,(#153208,#153209,#153210,#153211,#153212,
#153213,#153214,#153215),.UNSPECIFIED.,.F.,.F.,(4,1,1,1,1,4),(72.2566310325654,
72.3311409496812,73.3299773996431,74.3288138496049,75.3276502995668,76.3138963582499),
 .UNSPECIFIED.);
#1625=B_SPLINE_CURVE_WITH_KNOTS('',3,(#153221,#153222,#153223,#153224,#153225,
#153226,#153227,#153228,#153229,#153230,#153231,#153232,#153233,#153234,
#153235,#153236,#153237,#153238,#153239,#153240,#153241,#153242,#153243,
#153244,#153245,#153246,#153247,#153248,#153249,#153250,#153251,#153252,
#153253,#153254,#153255,#153256,#153257,#153258,#153259,#153260,#153261,
#153262,#153263,#153264,#153265,#153266,#153267,#153268,#153269,#153270,
#153271,#153272,#153273,#153274,#153275,#153276,#153277,#153278,#153279,
#153280,#153281,#153282,#153283,#153284,#153285,#153286,#153287,#153288,
#153289,#153290,#153291,#153292,#153293,#153294,#153295,#153296,#153297,
#153298,#153299,#153300,#153301,#153302,#153303,#153304,#153305,#153306,
#153307,#153308,#153309,#153310,#153311,#153312,#153313,#153314,#153315,
#153316,#153317,#153318,#153319,#153320,#153321,#153322,#153323,#153324,
#153325,#153326,#153327,#153328,#153329,#153330,#153331,#153332,#153333,
#153334,#153335,#153336,#153337,#153338,#153339,#153340,#153341,#153342,
#153343,#153344),.UNSPECIFIED.,.F.,.F.,(4,3,3,3,3,3,3,3,3,3,3,3,3,3,3,3,
3,3,3,3,3,3,3,3,3,3,3,3,3,3,3,3,3,3,3,3,3,3,3,3,3,4),(78.5398164398063,
78.6677108218491,78.788966381972,78.8875645069757,78.9860222897523,79.086244857525,
79.1845244152532,79.2827709943266,79.3810140773651,79.4827112660073,79.5810956794261,
79.68444925568,79.7878028319339,79.8864009569376,79.9848587397144,80.0850813074871,
80.1833608652152,80.2816074442886,80.3798505273271,80.4815477159693,80.5799321293881,
80.6832857056419,80.7866392818958,80.8852374068995,80.9836951896763,81.0839177574489,
81.1821973151771,81.2804438942504,81.3786869772889,81.4803841659311,81.5787685793499,
81.6821221556038,81.7854757318576,81.8868624768865,81.9852993359155,82.0836394970758,
82.1819125591245,82.2801480487663,82.3784063346505,82.4766798010887,82.5750347961583,
82.5965696920888),.UNSPECIFIED.);
#1626=B_SPLINE_CURVE_WITH_KNOTS('',3,(#153345,#153346,#153347,#153348,#153349,
#153350),.UNSPECIFIED.,.F.,.F.,(4,1,1,4),(76.3138574014144,76.7912934820483,
77.7901299320101,78.539816339745),.UNSPECIFIED.);
#1627=B_SPLINE_CURVE_WITH_KNOTS('',3,(#153352,#153353,#153354,#153355,#153356,
#153357,#153358),.UNSPECIFIED.,.F.,.F.,(4,1,1,1,4),(76.3138963582499,76.3264867495287,
77.3253231994906,78.3241596494524,78.539816339745),.UNSPECIFIED.);
#1628=B_SPLINE_CURVE_WITH_KNOTS('',3,(#153359,#153360,#153361,#153362,#153363,
#153364,#153365,#153366,#153367,#153368,#153369,#153370,#153371,#153372,
#153373,#153374,#153375,#153376,#153377,#153378,#153379,#153380,#153381,
#153382,#153383,#153384,#153385,#153386,#153387,#153388,#153389,#153390,
#153391,#153392,#153393,#153394,#153395,#153396,#153397,#153398,#153399,
#153400,#153401,#153402,#153403,#153404,#153405,#153406,#153407,#153408,
#153409,#153410,#153411,#153412,#153413,#153414,#153415,#153416,#153417,
#153418,#153419,#153420,#153421,#153422,#153423,#153424,#153425,#153426,
#153427,#153428,#153429,#153430,#153431,#153432,#153433,#153434,#153435,
#153436,#153437,#153438,#153439,#153440,#153441,#153442,#153443,#153444,
#153445,#153446,#153447,#153448,#153449,#153450,#153451,#153452,#153453,
#153454,#153455,#153456,#153457,#153458,#153459,#153460,#153461,#153462,
#153463,#153464,#153465,#153466,#153467,#153468,#153469,#153470,#153471,
#153472,#153473,#153474,#153475,#153476,#153477,#153478,#153479,#153480,
#153481,#153482),.UNSPECIFIED.,.F.,.F.,(4,3,3,3,3,3,3,3,3,3,3,3,3,3,3,3,
3,3,3,3,3,3,3,3,3,3,3,3,3,3,3,3,3,3,3,3,3,3,3,3,3,4),(78.539816339745,78.6377138097037,
78.7346673304386,78.8315786913982,78.9284788661298,79.0271081744509,79.1241353185132,
79.2235657089638,79.3229960994143,79.421594224418,79.5200520071948,79.6202745749675,
79.7185541326956,79.8168007117689,79.9150437948075,80.0167409834497,80.1151253968685,
80.2184789731223,80.3218325493762,80.4204306743799,80.5188884571567,80.6191110249294,
80.7173905826575,80.8156371617309,80.9138802447694,81.0155774334116,81.1139618468304,
81.2173154230842,81.3206689993381,81.4192671243418,81.5177249071184,81.6179474748911,
81.7162270326193,81.8144736116927,81.9127166947311,82.0144138833733,82.1127982967921,
82.216151873046,82.3195054492999,82.4180964130078,82.5165362141558,82.5977152335624),
 .UNSPECIFIED.);
#1629=B_SPLINE_CURVE_WITH_KNOTS('',3,(#153488,#153489,#153490,#153491,#153492,
#153493,#153494,#153495),.UNSPECIFIED.,.F.,.F.,(4,1,1,1,1,4),(84.8230070320566,
85.7808215317051,86.779657981667,87.7784944316289,88.7773308815908,88.8809435133539),
 .UNSPECIFIED.);
#1630=B_SPLINE_CURVE_WITH_KNOTS('',3,(#153496,#153497,#153498,#153499,#153500,
#153501,#153502,#153503,#153504,#153505,#153506,#153507,#153508,#153509,
#153510,#153511,#153512,#153513,#153514,#153515,#153516,#153517,#153518,
#153519,#153520,#153521,#153522,#153523,#153524,#153525,#153526,#153527,
#153528,#153529,#153530,#153531,#153532,#153533,#153534,#153535,#153536,
#153537,#153538,#153539,#153540,#153541,#153542,#153543,#153544,#153545,
#153546,#153547,#153548,#153549,#153550,#153551,#153552,#153553,#153554,
#153555,#153556,#153557,#153558,#153559,#153560,#153561,#153562,#153563,
#153564,#153565),.UNSPECIFIED.,.F.,.F.,(4,3,3,3,3,3,3,3,3,3,3,3,3,3,3,3,
3,3,3,3,3,3,3,4),(82.5965696920888,82.695141358,82.7843121818195,82.8829103068232,
82.9813680895999,83.0815906573726,83.1798702151008,83.2781167941742,83.3763598772127,
83.4780570658548,83.5764414792737,83.6797950555275,83.7831486317814,83.8817467567851,
83.9802045395617,84.0804271073344,84.1787066650625,84.2769532441359,84.3751963271743,
84.4768935158166,84.5752779292353,84.6786315054893,84.7819850817433,84.8230016469246),
 .UNSPECIFIED.);
#1631=B_SPLINE_CURVE_WITH_KNOTS('',3,(#153567,#153568,#153569,#153570,#153571,
#153572,#153573,#153574,#153575,#153576,#153577,#153578,#153579,#153580,
#153581,#153582,#153583,#153584,#153585,#153586,#153587,#153588,#153589,
#153590,#153591,#153592,#153593,#153594,#153595,#153596,#153597,#153598,
#153599,#153600,#153601,#153602,#153603,#153604,#153605,#153606,#153607,
#153608,#153609,#153610,#153611,#153612,#153613,#153614,#153615,#153616,
#153617,#153618,#153619,#153620,#153621,#153622,#153623,#153624,#153625,
#153626,#153627,#153628,#153629,#153630,#153631,#153632,#153633,#153634,
#153635,#153636),.UNSPECIFIED.,.F.,.F.,(4,3,3,3,3,3,3,3,3,3,3,3,3,3,3,3,
3,3,3,3,3,3,3,4),(82.5977152335624,82.6960046045216,82.7942552746611,82.8924967320984,
82.9907584472983,83.0891304035499,83.1875670560788,83.2861621230254,83.3183418992618,
83.4169400242655,83.5153978070419,83.6156203748146,83.7138999325428,83.8121465116162,
83.9103895946549,84.0120867832971,84.1104711967159,84.2138247729698,84.3171783492237,
84.4205578302504,84.5236543867486,84.6265834813177,84.7292989065991,84.8230016469246),
 .UNSPECIFIED.);
#1632=B_SPLINE_CURVE_WITH_KNOTS('',3,(#153637,#153638,#153639,#153640,#153641,
#153642,#153643,#153644,#153645,#153646,#153647,#153648,#153649,#153650,
#153651,#153652,#153653,#153654,#153655,#153656,#153657,#153658,#153659,
#153660,#153661,#153662,#153663,#153664,#153665,#153666,#153667,#153668,
#153669,#153670,#153671,#153672,#153673,#153674,#153675,#153676,#153677,
#153678,#153679,#153680,#153681,#153682,#153683,#153684,#153685,#153686,
#153687,#153688,#153689,#153690,#153691,#153692,#153693,#153694,#153695,
#153696,#153697,#153698,#153699,#153700,#153701,#153702,#153703,#153704,
#153705,#153706,#153707,#153708,#153709,#153710,#153711,#153712,#153713,
#153714,#153715,#153716,#153717,#153718,#153719,#153720,#153721,#153722,
#153723,#153724,#153725,#153726,#153727,#153728,#153729,#153730,#153731,
#153732,#153733,#153734,#153735,#153736,#153737,#153738,#153739,#153740,
#153741,#153742,#153743,#153744,#153745,#153746,#153747,#153748,#153749,
#153750,#153751,#153752,#153753,#153754,#153755,#153756,#153757,#153758,
#153759,#153760),.UNSPECIFIED.,.F.,.F.,(4,3,3,3,3,3,3,3,3,3,3,3,3,3,3,3,
3,3,3,3,3,3,3,3,3,3,3,3,3,3,3,3,3,3,3,3,3,3,3,3,3,4),(84.8230016472006,
84.9261861619506,85.0296647966982,85.1332945907094,85.2372126194226,85.3160147991856,
85.4146129241893,85.5130707069661,85.6132932747388,85.7115728324669,85.8098194115403,
85.9080624945788,86.0097596832209,86.1081440966397,86.2114976728936,86.3148512491474,
86.4134493741511,86.5119071569279,86.6121297247006,86.7104092824287,86.8086558615021,
86.9068989445406,87.0085961331827,87.1069805466016,87.2103341228554,87.3136876991093,
87.412285824113,87.5107436068898,87.6109661746624,87.7092457323906,87.807492311464,
87.9057353945025,88.0074325831446,88.1058169965635,88.2091705728173,88.3125241490712,
88.4111137865082,88.5095698168674,88.6079122101949,88.7061871882943,88.8044419893836,
88.8801389091725),.UNSPECIFIED.);
#1633=B_SPLINE_CURVE_WITH_KNOTS('',3,(#153766,#153767,#153768,#153769,#153770,
#153771,#153772,#153773,#153774,#153775,#153776,#153777,#153778,#153779,
#153780,#153781,#153782,#153783,#153784,#153785,#153786,#153787,#153788,
#153789,#153790,#153791,#153792,#153793,#153794,#153795,#153796,#153797,
#153798,#153799,#153800,#153801,#153802,#153803,#153804,#153805,#153806,
#153807,#153808,#153809,#153810,#153811,#153812,#153813,#153814,#153815,
#153816,#153817,#153818,#153819,#153820,#153821,#153822,#153823,#153824,
#153825,#153826,#153827,#153828,#153829,#153830,#153831,#153832,#153833,
#153834,#153835,#153836,#153837,#153838,#153839,#153840,#153841,#153842,
#153843,#153844,#153845,#153846,#153847,#153848,#153849,#153850,#153851,
#153852,#153853,#153854,#153855,#153856,#153857,#153858,#153859,#153860,
#153861,#153862,#153863,#153864,#153865,#153866,#153867,#153868,#153869,
#153870,#153871,#153872,#153873,#153874,#153875,#153876,#153877,#153878,
#153879,#153880,#153881,#153882,#153883,#153884,#153885,#153886,#153887,
#153888,#153889),.UNSPECIFIED.,.F.,.F.,(4,3,3,3,3,3,3,3,3,3,3,3,3,3,3,3,
3,3,3,3,3,3,3,3,3,3,3,3,3,3,3,3,3,3,3,3,3,3,3,3,3,4),(91.1061869541041,
91.204341964477,91.3024795334308,91.400629164884,91.4988897541857,91.5972075103079,
91.6957053368615,91.7738402314764,91.8724383564801,91.9708961392568,92.0711187070295,
92.1693982647576,92.267644843831,92.3658879268695,92.4675851155117,92.5659695289306,
92.6693231051844,92.7726766814383,92.871274806442,92.9697325892188,93.0699551569915,
93.1682347147196,93.2664812937929,93.3647243768313,93.4664215654735,93.5648059788923,
93.6681595551462,93.7715131314001,93.8701112564038,93.9685690391805,94.0687916069532,
94.1670711646814,94.2653177437547,94.3635608267932,94.4652580154354,94.5636424288543,
94.6669960051081,94.770349581362,94.8689185475107,94.9673651080125,95.0657083030554,
95.1638472961989),.UNSPECIFIED.);
#1634=B_SPLINE_CURVE_WITH_KNOTS('',3,(#153890,#153891,#153892,#153893,#153894,
#153895),.UNSPECIFIED.,.F.,.F.,(4,1,1,4),(88.8809435133539,89.7761673315526,
90.7750037815145,91.1061798192275),.UNSPECIFIED.);
#1635=B_SPLINE_CURVE_WITH_KNOTS('',3,(#153897,#153898,#153899,#153900,#153901,
#153902,#153903,#153904,#153905,#153906,#153907,#153908,#153909,#153910,
#153911,#153912,#153913,#153914,#153915,#153916,#153917,#153918,#153919,
#153920,#153921,#153922,#153923,#153924,#153925,#153926,#153927,#153928,
#153929,#153930,#153931,#153932,#153933,#153934,#153935,#153936,#153937,
#153938,#153939,#153940,#153941,#153942,#153943,#153944,#153945,#153946,
#153947,#153948,#153949,#153950,#153951,#153952,#153953,#153954,#153955,
#153956,#153957,#153958,#153959,#153960,#153961,#153962,#153963,#153964,
#153965,#153966,#153967,#153968,#153969),.UNSPECIFIED.,.F.,.F.,(4,3,3,3,
3,3,3,3,3,3,3,3,3,3,3,3,3,3,3,3,3,3,3,3,4),(88.8801389091725,88.9783987534772,
89.0767679360319,89.1752003650069,89.2737927525417,89.3113605990331,89.4099587240368,
89.5084165068135,89.6086390745862,89.7069186323143,89.8051652113877,89.9034082944262,
90.0051054830683,90.1034898964871,90.206843472741,90.3101970489949,90.409695787095,
90.5067185530535,90.6036495481491,90.7005198981798,90.8019366620839,90.8988156754796,
90.9957205549586,91.0927209416411,91.1061869537961),.UNSPECIFIED.);
#1636=B_SPLINE_CURVE_WITH_KNOTS('',3,(#153970,#153971,#153972,#153973,#153974,
#153975,#153976,#153977,#153978,#153979,#153980,#153981,#153982,#153983,
#153984,#153985,#153986,#153987,#153988,#153989,#153990,#153991,#153992,
#153993,#153994,#153995,#153996,#153997,#153998,#153999,#154000,#154001,
#154002,#154003,#154004,#154005,#154006,#154007,#154008,#154009,#154010,
#154011,#154012,#154013,#154014,#154015,#154016,#154017,#154018,#154019,
#154020,#154021,#154022,#154023,#154024,#154025,#154026,#154027,#154028,
#154029,#154030,#154031,#154032,#154033,#154034,#154035,#154036,#154037,
#154038,#154039,#154040,#154041,#154042,#154043,#154044,#154045,#154046,
#154047,#154048,#154049,#154050,#154051,#154052,#154053,#154054,#154055,
#154056,#154057,#154058,#154059,#154060,#154061,#154062,#154063,#154064,
#154065,#154066,#154067,#154068,#154069,#154070,#154071,#154072,#154073,
#154074,#154075,#154076,#154077,#154078,#154079,#154080,#154081,#154082,
#154083,#154084,#154085,#154086,#154087,#154088,#154089,#154090,#154091,
#154092,#154093),.UNSPECIFIED.,.F.,.F.,(4,3,3,3,3,3,3,3,3,3,3,3,3,3,3,3,
3,3,3,3,3,3,3,3,3,3,3,3,3,3,3,3,3,3,3,3,3,3,3,3,3,4),(91.1061869541041,
91.2465035596771,91.3090334989568,91.4076316239605,91.5060894067374,91.60631197451,
91.7045915322382,91.8028381113116,91.9010811943501,92.0027783829923,92.101162796411,
92.2045163726649,92.3078699489187,92.4064680739224,92.5049258566991,92.6051484244718,
92.7034279822,92.8016745612733,92.8999176443118,93.001614832954,93.0999992463728,
93.2033528226267,93.3067063988806,93.4053045238843,93.5037623066611,93.6039848744337,
93.7022644321619,93.8005110112353,93.8987540942738,94.0004512829159,94.0988356963347,
94.2021892725886,94.3055428488424,94.4041508037272,94.5025891903085,94.6009312472761,
94.6992065724929,94.7974446925405,94.895715960323,94.9940021459656,95.0923959721231,
95.1629909128946),.UNSPECIFIED.);
#1637=B_SPLINE_CURVE_WITH_KNOTS('',3,(#154099,#154100,#154101,#154102,#154103,
#154104,#154105,#154106),.UNSPECIFIED.,.F.,.F.,(4,1,1,1,1,4),(97.3893797693875,
97.7668589312476,98.7656953812095,99.7645318311714,100.763368281133,101.445901947532),
 .UNSPECIFIED.);
#1638=B_SPLINE_CURVE_WITH_KNOTS('',3,(#154107,#154108,#154109,#154110,#154111,
#154112,#154113,#154114,#154115,#154116,#154117,#154118,#154119,#154120,
#154121,#154122,#154123,#154124,#154125,#154126,#154127,#154128,#154129,
#154130,#154131,#154132,#154133,#154134,#154135,#154136,#154137,#154138,
#154139,#154140,#154141,#154142,#154143,#154144,#154145,#154146,#154147,
#154148,#154149,#154150,#154151,#154152,#154153,#154154,#154155,#154156,
#154157,#154158,#154159,#154160,#154161,#154162,#154163,#154164,#154165,
#154166,#154167,#154168,#154169,#154170,#154171,#154172,#154173,#154174,
#154175,#154176,#154177,#154178,#154179),.UNSPECIFIED.,.F.,.F.,(4,3,3,3,
3,3,3,3,3,3,3,3,3,3,3,3,3,3,3,3,3,3,3,3,4),(95.1638472961989,95.2620942640701,
95.3603371179254,95.4625493462751,95.5609328596376,95.659386716781,95.7579931491462,
95.7691860313239,95.8677841563277,95.9662419391048,96.0664645068774,96.1647440646056,
96.262990643679,96.3612337267176,96.4629309153596,96.5613153287785,96.6646689050321,
96.7680224812858,96.8674993725789,96.9668292609827,97.0660403563899,97.1651524247994,
97.2642075332238,97.3632407686269,97.3893722612837),.UNSPECIFIED.);
#1639=B_SPLINE_CURVE_WITH_KNOTS('',3,(#154181,#154182,#154183,#154184,#154185,
#154186,#154187,#154188,#154189,#154190,#154191,#154192,#154193,#154194,
#154195,#154196,#154197,#154198,#154199,#154200,#154201,#154202,#154203,
#154204,#154205,#154206,#154207,#154208,#154209,#154210,#154211,#154212,
#154213,#154214,#154215,#154216,#154217,#154218,#154219,#154220,#154221,
#154222,#154223,#154224,#154225,#154226,#154227,#154228,#154229,#154230,
#154231,#154232,#154233,#154234,#154235,#154236,#154237,#154238,#154239,
#154240,#154241,#154242,#154243,#154244,#154245,#154246,#154247,#154248,
#154249,#154250),.UNSPECIFIED.,.F.,.F.,(4,3,3,3,3,3,3,3,3,3,3,3,3,3,3,3,
3,3,3,3,3,3,3,4),(95.1629909128946,95.2615807925411,95.3043792988043,95.402977423808,
95.5014352065848,95.6016577743575,95.6999373320856,95.798183911159,95.8964269941974,
95.9981241828396,96.0965085962584,96.1998621725123,96.3032157487662,96.4018138737699,
96.5002716565467,96.6004942243194,96.6987737820475,96.7970203611209,96.8952634441594,
96.9969606328015,97.0953450462203,97.1986986224742,97.302052198728,97.3893722612837),
 .UNSPECIFIED.);
#1640=B_SPLINE_CURVE_WITH_KNOTS('',3,(#154251,#154252,#154253,#154254,#154255,
#154256,#154257,#154258),.UNSPECIFIED.,.F.,.F.,(4,1,1,1,1,4),(97.3893809708947,
98.3008886486899,99.2997250986518,100.298561548614,101.297397998576,101.447496608354),
 .UNSPECIFIED.);
#1641=B_SPLINE_CURVE_WITH_KNOTS('',3,(#154264,#154265,#154266,#154267,#154268,
#154269,#154270,#154271,#154272,#154273,#154274,#154275,#154276,#154277,
#154278,#154279,#154280,#154281,#154282,#154283,#154284,#154285,#154286,
#154287,#154288,#154289,#154290,#154291,#154292,#154293,#154294,#154295,
#154296,#154297,#154298,#154299,#154300,#154301,#154302,#154303,#154304,
#154305,#154306,#154307,#154308,#154309,#154310,#154311,#154312,#154313,
#154314,#154315,#154316,#154317,#154318,#154319,#154320,#154321,#154322,
#154323,#154324,#154325,#154326,#154327,#154328,#154329,#154330,#154331,
#154332,#154333,#154334,#154335,#154336,#154337,#154338,#154339,#154340,
#154341,#154342,#154343,#154344,#154345,#154346,#154347,#154348,#154349,
#154350,#154351,#154352,#154353,#154354,#154355,#154356,#154357,#154358,
#154359,#154360,#154361,#154362,#154363,#154364,#154365,#154366,#154367,
#154368,#154369,#154370,#154371,#154372,#154373,#154374,#154375,#154376,
#154377,#154378,#154379,#154380,#154381,#154382,#154383,#154384,#154385,
#154386,#154387),.UNSPECIFIED.,.F.,.F.,(4,3,3,3,3,3,3,3,3,3,3,3,3,3,3,3,
3,3,3,3,3,3,3,3,3,3,3,3,3,3,3,3,3,3,3,3,3,3,3,3,3,4),(103.672557568463,
103.759877631019,103.858475756023,103.956933538799,104.057156106572,104.1554356643,
104.253682243374,104.351925326412,104.453622515054,104.552006928473,104.655360504727,
104.758714080981,104.857312205985,104.955769988762,105.055992556534,105.154272114262,
105.252518693336,105.350761776374,105.452458965017,105.550843378435,105.654196954689,
105.757550530943,105.856148655947,105.954606438723,106.054829006496,106.153108564224,
106.251355143298,106.349598226336,106.451295414978,106.549679828397,106.653033404651,
106.756386980905,106.854986798951,106.953445809633,107.051788768345,107.150068003066,
107.248313037022,107.34655335305,107.444881222478,107.543251670412,107.641785788067,
107.729756514353),.UNSPECIFIED.);
#1642=B_SPLINE_CURVE_WITH_KNOTS('',3,(#154388,#154389,#154390,#154391,#154392,
#154393),.UNSPECIFIED.,.F.,.F.,(4,1,1,4),(101.445901947532,101.762204731095,
102.761041181057,103.672548858805),.UNSPECIFIED.);
#1643=B_SPLINE_CURVE_WITH_KNOTS('',3,(#154395,#154396,#154397,#154398,#154399,
#154400),.UNSPECIFIED.,.F.,.F.,(4,1,1,4),(101.447496608354,102.296234448537,
103.295070898499,103.672550060316),.UNSPECIFIED.);
#1644=B_SPLINE_CURVE_WITH_KNOTS('',3,(#154401,#154402,#154403,#154404,#154405,
#154406,#154407,#154408,#154409,#154410,#154411,#154412,#154413,#154414,
#154415,#154416,#154417,#154418,#154419,#154420,#154421,#154422,#154423,
#154424,#154425,#154426,#154427,#154428,#154429,#154430,#154431,#154432,
#154433,#154434,#154435,#154436,#154437,#154438,#154439,#154440,#154441,
#154442,#154443,#154444,#154445,#154446,#154447,#154448,#154449,#154450,
#154451,#154452,#154453,#154454,#154455,#154456,#154457,#154458,#154459,
#154460,#154461,#154462,#154463,#154464,#154465,#154466,#154467,#154468,
#154469,#154470,#154471,#154472,#154473,#154474,#154475,#154476,#154477,
#154478,#154479,#154480,#154481,#154482,#154483,#154484,#154485,#154486,
#154487,#154488,#154489,#154490,#154491,#154492,#154493,#154494,#154495,
#154496,#154497,#154498,#154499,#154500,#154501,#154502,#154503,#154504,
#154505,#154506,#154507,#154508,#154509,#154510,#154511,#154512,#154513,
#154514,#154515,#154516,#154517,#154518,#154519,#154520,#154521,#154522,
#154523,#154524,#154525,#154526,#154527),.UNSPECIFIED.,.F.,.F.,(4,3,3,3,
3,3,3,3,3,3,3,3,3,3,3,3,3,3,3,3,3,3,3,3,3,3,3,3,3,3,3,3,3,3,3,3,3,3,3,3,
3,3,4),(103.672557568463,103.771601702603,103.870660322484,103.96976131202,
104.06899945985,104.168318657834,104.267812431338,104.293907348461,104.392505473465,
104.490963256242,104.591185824014,104.689465381742,104.787711960816,104.885955043854,
104.987652232497,105.086036645915,105.189390222169,105.292743798423,105.391341923427,
105.489799706204,105.590022273976,105.688301831705,105.786548410778,105.884791493817,
105.986488682459,106.084873095877,106.188226672131,106.291580248385,106.390178373389,
106.488636156165,106.588858723938,106.687138281666,106.78538486074,106.883627943778,
106.98532513242,107.083709545839,107.187063122093,107.290416698347,107.389023062577,
107.487464394931,107.585810440439,107.684086111444,107.730086386038),
 .UNSPECIFIED.);
#1645=B_SPLINE_CURVE_WITH_KNOTS('',3,(#154533,#154534,#154535,#154536,#154537,
#154538,#154539,#154540,#154541,#154542,#154543,#154544,#154545,#154546,
#154547,#154548,#154549,#154550,#154551,#154552,#154553,#154554,#154555,
#154556,#154557,#154558,#154559,#154560,#154561,#154562,#154563,#154564,
#154565,#154566,#154567,#154568,#154569,#154570,#154571,#154572,#154573,
#154574,#154575,#154576,#154577,#154578,#154579,#154580,#154581,#154582,
#154583,#154584,#154585,#154586,#154587,#154588,#154589,#154590,#154591,
#154592,#154593,#154594,#154595,#154596,#154597,#154598,#154599,#154600,
#154601,#154602,#154603,#154604,#154605,#154606,#154607,#154608,#154609,
#154610,#154611,#154612,#154613,#154614,#154615,#154616,#154617,#154618,
#154619,#154620,#154621,#154622,#154623,#154624,#154625,#154626,#154627,
#154628,#154629,#154630,#154631,#154632,#154633,#154634,#154635,#154636,
#154637,#154638,#154639,#154640,#154641,#154642,#154643,#154644,#154645,
#154646,#154647,#154648,#154649,#154650,#154651,#154652,#154653,#154654,
#154655,#154656,#154657,#154658,#154659),.UNSPECIFIED.,.F.,.F.,(4,3,3,3,
3,3,3,3,3,3,3,3,3,3,3,3,3,3,3,3,3,3,3,3,3,3,3,3,3,3,3,3,3,3,3,3,3,3,3,3,
3,3,4),(109.955742875951,110.055241614051,110.152151423466,110.249014842069,
110.345862894414,110.447330365998,110.544300028994,110.641334438528,110.738518045248,
110.751732780752,110.850330905756,110.948788688532,111.049011256305,111.147290814033,
111.245537393107,111.343780476145,111.445477664787,111.543862078206,111.64721565446,
111.750569230714,111.849167355718,111.947625138494,112.047847706267,112.146127263995,
112.244373843069,112.342616926107,112.444314114749,112.542698528168,112.646052104422,
112.749405680676,112.84800380568,112.946461588456,113.046684156229,113.144963713957,
113.243210293031,113.341453376069,113.443150564711,113.54153497813,113.644888554384,
113.748242130638,113.846836224895,113.945278284723,114.013656770728),
 .UNSPECIFIED.);
#1646=B_SPLINE_CURVE_WITH_KNOTS('',3,(#154660,#154661,#154662,#154663,#154664,
#154665,#154666,#154667,#154668,#154669,#154670,#154671,#154672,#154673,
#154674,#154675,#154676,#154677,#154678,#154679,#154680,#154681,#154682,
#154683,#154684,#154685,#154686,#154687,#154688,#154689,#154690,#154691,
#154692,#154693,#154694,#154695,#154696,#154697,#154698,#154699,#154700,
#154701,#154702,#154703,#154704,#154705,#154706,#154707,#154708,#154709,
#154710,#154711,#154712,#154713,#154714,#154715,#154716,#154717,#154718,
#154719,#154720,#154721,#154722,#154723,#154724,#154725,#154726,#154727,
#154728,#154729),.UNSPECIFIED.,.F.,.F.,(4,3,3,3,3,3,3,3,3,3,3,3,3,3,3,3,
3,3,3,3,3,3,3,4),(107.729756514353,107.755223430866,107.85382155587,107.952279338646,
108.052501906419,108.150781464147,108.24902804322,108.347271126259,108.448968314901,
108.54735272832,108.650706304574,108.754059880828,108.852658005832,108.951115788609,
109.051338356381,109.149617914109,109.247864493183,109.346107576221,109.447804764864,
109.546189178282,109.649542754536,109.75289633079,109.893212936346,109.955742875643),
 .UNSPECIFIED.);
#1647=B_SPLINE_CURVE_WITH_KNOTS('',3,(#154731,#154732,#154733,#154734,#154735,
#154736,#154737,#154738,#154739,#154740,#154741,#154742,#154743,#154744,
#154745,#154746,#154747,#154748,#154749,#154750,#154751,#154752,#154753,
#154754,#154755,#154756,#154757,#154758,#154759,#154760,#154761,#154762,
#154763,#154764,#154765,#154766,#154767,#154768,#154769,#154770,#154771,
#154772,#154773,#154774,#154775,#154776,#154777,#154778,#154779,#154780,
#154781,#154782,#154783,#154784,#154785,#154786,#154787,#154788,#154789,
#154790,#154791,#154792,#154793,#154794,#154795,#154796,#154797,#154798,
#154799,#154800),.UNSPECIFIED.,.F.,.F.,(4,3,3,3,3,3,3,3,3,3,3,3,3,3,3,3,
3,3,3,3,3,3,3,4),(107.730086386038,107.82832774994,107.926578848836,108.024934135355,
108.123344660194,108.22192400452,108.289253148309,108.387851273313,108.48630905609,
108.586531623862,108.68481118159,108.783057760664,108.881300843702,108.982998032344,
109.081382445763,109.184736022017,109.288089598271,109.386591328536,109.484956309732,
109.583214317042,109.681399820024,109.779540599734,109.877698313765,109.955742875643),
 .UNSPECIFIED.);
#1648=B_SPLINE_CURVE_WITH_KNOTS('',3,(#154801,#154802,#154803,#154804,#154805,
#154806,#154807,#154808),.UNSPECIFIED.,.F.,.F.,(4,1,1,1,1,4),(109.955750010575,
110.286926048232,111.285762498194,112.284598948156,113.283435398118,114.012186908316),
 .UNSPECIFIED.);
#1649=B_SPLINE_CURVE_WITH_KNOTS('',3,(#154814,#154815,#154816,#154817,#154818,
#154819,#154820,#154821,#154822,#154823,#154824,#154825,#154826,#154827,
#154828,#154829,#154830,#154831,#154832,#154833,#154834,#154835,#154836,
#154837,#154838,#154839,#154840,#154841,#154842,#154843,#154844,#154845,
#154846,#154847,#154848,#154849,#154850,#154851,#154852,#154853,#154854,
#154855,#154856,#154857,#154858,#154859,#154860,#154861,#154862,#154863,
#154864,#154865,#154866,#154867,#154868,#154869,#154870,#154871,#154872,
#154873,#154874,#154875,#154876,#154877,#154878,#154879,#154880,#154881,
#154882,#154883,#154884,#154885,#154886,#154887,#154888,#154889,#154890,
#154891,#154892,#154893,#154894,#154895,#154896,#154897,#154898,#154899,
#154900,#154901,#154902,#154903,#154904,#154905,#154906,#154907,#154908,
#154909,#154910,#154911,#154912,#154913,#154914,#154915,#154916,#154917,
#154918,#154919,#154920,#154921,#154922,#154923,#154924,#154925,#154926,
#154927,#154928,#154929,#154930,#154931,#154932,#154933,#154934,#154935,
#154936,#154937),.UNSPECIFIED.,.F.,.F.,(4,3,3,3,3,3,3,3,3,3,3,3,3,3,3,3,
3,3,3,3,3,3,3,3,3,3,3,3,3,3,3,3,3,3,3,3,3,3,3,3,3,4),(116.238928182823,
116.341566510357,116.44447107289,116.547509821617,116.650828963887,116.744751480523,
116.843349605527,116.941807388303,117.042029956076,117.140309513804,117.238556092877,
117.336799175916,117.438496364558,117.536880777977,117.640234354231,117.743587930485,
117.842186055489,117.940643838266,118.040866406038,118.139145963766,118.23739254284,
118.335635625878,118.437332814521,118.53571722794,118.639070804193,118.742424380447,
118.841022505451,118.939480288227,119.039702856,119.137982413728,119.236228992802,
119.33447207584,119.436169264482,119.534553677901,119.637907254155,119.741260830409,
119.839851983063,119.938309194714,120.036651331122,120.134925920028,120.233176074189,
120.296103360098),.UNSPECIFIED.);
#1650=B_SPLINE_CURVE_WITH_KNOTS('',3,(#154938,#154939,#154940,#154941,#154942,
#154943,#154944,#154945,#154946,#154947,#154948,#154949,#154950,#154951,
#154952,#154953,#154954,#154955,#154956,#154957,#154958,#154959,#154960,
#154961,#154962,#154963,#154964,#154965,#154966,#154967,#154968,#154969,
#154970,#154971,#154972,#154973,#154974,#154975,#154976,#154977,#154978,
#154979,#154980,#154981,#154982,#154983,#154984,#154985,#154986,#154987,
#154988,#154989,#154990,#154991,#154992,#154993,#154994,#154995,#154996,
#154997,#154998,#154999,#155000,#155001,#155002,#155003,#155004,#155005,
#155006,#155007),.UNSPECIFIED.,.F.,.F.,(4,3,3,3,3,3,3,3,3,3,3,3,3,3,3,3,
3,3,3,3,3,3,3,4),(114.013656770728,114.111953348359,114.21020738509,114.308448373286,
114.406705784207,114.50507127457,114.60349801372,114.702086869152,114.747078580599,
114.845676705603,114.944134488379,115.044357056152,115.14263661388,115.240883192953,
115.339126275992,115.440823464634,115.539207878053,115.642561454307,115.745915030561,
115.84988875933,115.953561696348,116.057054365165,116.160309146372,116.238928182547),
 .UNSPECIFIED.);
#1651=B_SPLINE_CURVE_WITH_KNOTS('',3,(#155009,#155010,#155011,#155012,#155013,
#155014),.UNSPECIFIED.,.F.,.F.,(4,1,1,4),(114.012186908316,114.28227184808,
115.281108298042,116.238922797716),.UNSPECIFIED.);
#1652=B_SPLINE_CURVE_WITH_KNOTS('',3,(#155015,#155016,#155017,#155018,#155019,
#155020,#155021,#155022,#155023,#155024,#155025,#155026,#155027,#155028,
#155029,#155030,#155031,#155032,#155033,#155034,#155035,#155036,#155037,
#155038,#155039,#155040,#155041,#155042,#155043,#155044,#155045,#155046,
#155047,#155048,#155049,#155050,#155051,#155052,#155053,#155054,#155055,
#155056,#155057,#155058,#155059,#155060,#155061,#155062,#155063,#155064,
#155065,#155066,#155067,#155068,#155069,#155070,#155071,#155072,#155073,
#155074,#155075,#155076,#155077,#155078,#155079,#155080,#155081,#155082,
#155083,#155084,#155085,#155086,#155087,#155088,#155089,#155090,#155091,
#155092,#155093,#155094,#155095,#155096,#155097,#155098,#155099,#155100,
#155101,#155102,#155103,#155104,#155105,#155106,#155107,#155108,#155109,
#155110,#155111,#155112,#155113,#155114,#155115,#155116,#155117,#155118,
#155119,#155120,#155121,#155122,#155123,#155124,#155125,#155126,#155127,
#155128,#155129,#155130,#155131,#155132,#155133,#155134,#155135,#155136,
#155137,#155138,#155139,#155140,#155141),.UNSPECIFIED.,.F.,.F.,(4,3,3,3,
3,3,3,3,3,3,3,3,3,3,3,3,3,3,3,3,3,3,3,3,3,3,3,3,3,3,3,3,3,3,3,3,3,3,3,3,
3,3,4),(116.238928182823,116.279944748004,116.378542873008,116.477000655784,
116.577223223557,116.675502781285,116.773749360358,116.871992443397,116.973689632039,
117.072074045458,117.175427621712,117.278781197966,117.37737932297,117.475837105746,
117.576059673519,117.674339231247,117.77258581032,117.870828893359,117.972526082001,
118.07091049542,118.174264071673,118.277617647927,118.376215772931,118.474673555707,
118.57489612348,118.673175681208,118.771422260282,118.86966534332,118.971362531962,
119.069746945381,119.173100521635,119.276454097889,119.375052222893,119.47351000567,
119.573732573442,119.67201213117,119.770258710244,119.868501793282,119.970198981924,
120.068583395343,120.171936971597,120.275290547851,120.296396878359),
 .UNSPECIFIED.);
#1653=B_SPLINE_CURVE_WITH_KNOTS('',3,(#155147,#155148,#155149,#155150,#155151,
#155152,#155153,#155154),.UNSPECIFIED.,.F.,.F.,(4,1,1,1,1,4),(122.522113490002,
122.737770180294,123.736606630256,124.735443080218,125.73427953018,126.578666779634),
 .UNSPECIFIED.);
#1654=B_SPLINE_CURVE_WITH_KNOTS('',3,(#155155,#155156,#155157,#155158,#155159,
#155160,#155161,#155162,#155163,#155164,#155165,#155166,#155167,#155168,
#155169,#155170,#155171,#155172,#155173,#155174,#155175,#155176,#155177,
#155178,#155179,#155180,#155181,#155182,#155183,#155184,#155185,#155186,
#155187,#155188,#155189,#155190,#155191,#155192,#155193,#155194,#155195,
#155196,#155197,#155198,#155199,#155200,#155201,#155202,#155203,#155204,
#155205,#155206,#155207,#155208,#155209,#155210,#155211,#155212,#155213,
#155214,#155215,#155216,#155217,#155218,#155219,#155220,#155221,#155222,
#155223,#155224),.UNSPECIFIED.,.F.,.F.,(4,3,3,3,3,3,3,3,3,3,3,3,3,3,3,3,
3,3,3,3,3,3,3,4),(120.296103360098,120.394359113849,120.492722024964,120.591144738723,
120.689731152633,120.740097280371,120.838695405375,120.937153188151,121.037375755924,
121.135655313652,121.233901892726,121.332144975764,121.433842164407,121.532226577825,
121.635580154079,121.738933730333,121.836831200292,121.933909156543,122.030894120917,
122.127817176648,122.226391254986,122.323316910845,122.422715200424,122.522113490002),
 .UNSPECIFIED.);
#1655=B_SPLINE_CURVE_WITH_KNOTS('',3,(#155226,#155227,#155228,#155229,#155230,
#155231,#155232,#155233,#155234,#155235,#155236,#155237,#155238,#155239,
#155240,#155241,#155242,#155243,#155244,#155245,#155246,#155247,#155248,
#155249,#155250,#155251,#155252,#155253,#155254,#155255,#155256,#155257,
#155258,#155259,#155260,#155261,#155262,#155263,#155264,#155265,#155266,
#155267,#155268,#155269,#155270,#155271,#155272,#155273,#155274,#155275,
#155276,#155277,#155278,#155279,#155280,#155281,#155282,#155283,#155284,
#155285,#155286,#155287,#155288,#155289,#155290,#155291,#155292),
 .UNSPECIFIED.,.F.,.F.,(4,3,3,3,3,3,3,3,3,3,3,3,3,3,3,3,3,3,3,3,3,3,4),
(120.296396878359,120.394962212568,120.493394239118,120.591721801248,120.689992619365,
120.788236205456,120.886482037624,120.984827514811,121.083221502001,121.181792188648,
121.274126997813,121.372725122817,121.471182905593,121.571405473366,121.669685031094,
121.767931610168,121.866174693206,121.967871881848,122.066256295267,122.169609871521,
122.272963447775,122.400857829824,122.522113389936),.UNSPECIFIED.);
#1656=B_SPLINE_CURVE_WITH_KNOTS('',3,(#155293,#155294,#155295,#155296,#155297,
#155298,#155299,#155300),.UNSPECIFIED.,.F.,.F.,(4,1,1,1,1,4),(122.522113490002,
123.271799897737,124.270636347699,125.269472797661,126.268309247622,126.580285712868),
 .UNSPECIFIED.);
#1657=B_SPLINE_CURVE_WITH_KNOTS('',3,(#155306,#155307,#155308,#155309,#155310,
#155311,#155312,#155313,#155314,#155315,#155316,#155317,#155318,#155319,
#155320,#155321,#155322,#155323,#155324,#155325,#155326,#155327,#155328,
#155329,#155330,#155331,#155332,#155333,#155334,#155335,#155336,#155337,
#155338,#155339,#155340,#155341,#155342,#155343,#155344,#155345,#155346,
#155347,#155348,#155349,#155350,#155351,#155352,#155353,#155354,#155355,
#155356,#155357,#155358,#155359,#155360,#155361,#155362,#155363,#155364,
#155365,#155366,#155367,#155368,#155369,#155370,#155371,#155372,#155373,
#155374,#155375,#155376,#155377,#155378,#155379,#155380,#155381,#155382,
#155383,#155384,#155385,#155386,#155387,#155388,#155389,#155390,#155391,
#155392,#155393,#155394,#155395,#155396,#155397,#155398,#155399,#155400,
#155401,#155402,#155403,#155404,#155405,#155406,#155407,#155408,#155409,
#155410,#155411,#155412,#155413,#155414,#155415,#155416,#155417,#155418,
#155419,#155420,#155421,#155422,#155423,#155424,#155425,#155426,#155427,
#155428,#155429,#155430,#155431,#155432),.UNSPECIFIED.,.F.,.F.,(4,3,3,3,
3,3,3,3,3,3,3,3,3,3,3,3,3,3,3,3,3,3,3,3,3,3,3,3,3,3,3,3,3,3,3,3,3,3,3,3,
3,3,4),(128.805298797182,128.902840431273,129.000250613517,129.097560812666,
129.194818343698,129.292053887498,129.389298094495,129.486642967569,129.584044330746,
129.681605924981,129.729625330028,129.828223455032,129.926681237808,130.026903805581,
130.125183363309,130.223429942382,130.321673025421,130.423370214063,130.521754627482,
130.625108203735,130.728461779989,130.827059904993,130.925517687769,131.025740255542,
131.12401981327,131.222266392343,131.320509475382,131.422206664024,131.520591077443,
131.623944653697,131.727298229951,131.825896354955,131.924354137731,132.024576705504,
132.122856263232,132.221102842306,132.319345925344,132.421043113987,132.519427527405,
132.622781103659,132.726134679913,132.824726637228,132.863178333069),
 .UNSPECIFIED.);
#1658=B_SPLINE_CURVE_WITH_KNOTS('',3,(#155433,#155434,#155435,#155436,#155437,
#155438,#155439),.UNSPECIFIED.,.F.,.F.,(4,1,1,1,4),(126.578666779634,126.733115980142,
127.731952430104,128.730788880066,128.805298797182),.UNSPECIFIED.);
#1659=B_SPLINE_CURVE_WITH_KNOTS('',3,(#155441,#155442,#155443,#155444,#155445,
#155446),.UNSPECIFIED.,.F.,.F.,(4,1,1,4),(126.580285712868,127.267145697584,
128.265982147546,128.805298797182),.UNSPECIFIED.);
#1660=B_SPLINE_CURVE_WITH_KNOTS('',3,(#155447,#155448,#155449,#155450,#155451,
#155452,#155453,#155454,#155455,#155456,#155457,#155458,#155459,#155460,
#155461,#155462,#155463,#155464,#155465,#155466,#155467,#155468,#155469,
#155470,#155471,#155472,#155473,#155474,#155475,#155476,#155477,#155478,
#155479,#155480,#155481,#155482,#155483,#155484,#155485,#155486,#155487,
#155488,#155489,#155490,#155491,#155492,#155493,#155494,#155495,#155496,
#155497,#155498,#155499,#155500,#155501,#155502,#155503,#155504,#155505,
#155506,#155507,#155508,#155509,#155510,#155511,#155512,#155513,#155514,
#155515,#155516,#155517,#155518,#155519,#155520,#155521,#155522,#155523,
#155524,#155525,#155526,#155527,#155528,#155529,#155530,#155531,#155532,
#155533,#155534,#155535,#155536,#155537,#155538,#155539,#155540,#155541,
#155542,#155543,#155544,#155545,#155546,#155547,#155548,#155549,#155550,
#155551,#155552,#155553,#155554,#155555,#155556,#155557,#155558,#155559,
#155560,#155561,#155562,#155563,#155564,#155565,#155566,#155567,#155568,
#155569,#155570),.UNSPECIFIED.,.F.,.F.,(4,3,3,3,3,3,3,3,3,3,3,3,3,3,3,3,
3,3,3,3,3,3,3,3,3,3,3,3,3,3,3,3,3,3,3,3,3,3,3,3,3,4),(128.805299011168,
128.910085619878,129.015255759158,129.12063010964,129.226318351055,129.264818597508,
129.363416722512,129.461874505288,129.562097073061,129.660376630789,129.758623209863,
129.856866292901,129.958563481543,130.056947894962,130.160301471216,130.26365504747,
130.362253172474,130.46071095525,130.560933523023,130.659213080751,130.757459659825,
130.855702742863,130.957399931505,131.055784344924,131.159137921178,131.262491497432,
131.361089622436,131.459547405213,131.559769972985,131.658049530713,131.756296109787,
131.854539192826,131.956236381468,132.054620794887,132.15797437114,132.261327947394,
132.359913784705,132.458366887944,132.559360477805,132.657635681036,132.759988464213,
132.86234124739),.UNSPECIFIED.);
#1661=B_SPLINE_CURVE_WITH_KNOTS('',3,(#155576,#155577,#155578,#155579,#155580,
#155581,#155582,#155583,#155584,#155585,#155586,#155587,#155588,#155589,
#155590,#155591,#155592,#155593,#155594,#155595,#155596,#155597,#155598,
#155599,#155600,#155601,#155602,#155603,#155604,#155605,#155606,#155607,
#155608,#155609,#155610,#155611,#155612,#155613,#155614,#155615,#155616,
#155617,#155618,#155619,#155620,#155621,#155622,#155623,#155624,#155625,
#155626,#155627,#155628,#155629,#155630,#155631,#155632,#155633,#155634,
#155635,#155636,#155637,#155638,#155639,#155640,#155641,#155642,#155643,
#155644,#155645,#155646,#155647,#155648,#155649,#155650,#155651,#155652,
#155653,#155654,#155655,#155656,#155657,#155658,#155659,#155660,#155661,
#155662,#155663,#155664,#155665,#155666,#155667,#155668,#155669,#155670,
#155671,#155672,#155673,#155674,#155675,#155676,#155677,#155678,#155679,
#155680,#155681,#155682,#155683,#155684,#155685,#155686,#155687,#155688,
#155689,#155690,#155691,#155692,#155693,#155694,#155695,#155696,#155697,
#155698,#155699,#155700,#155701,#155702),.UNSPECIFIED.,.F.,.F.,(4,3,3,3,
3,3,3,3,3,3,3,3,3,3,3,3,3,3,3,3,3,3,3,3,3,3,3,3,3,3,3,3,3,3,3,3,3,3,3,3,
3,3,4),(135.088484104361,135.187254556185,135.286029876603,135.384838499173,
135.483776463585,135.582788468007,135.681976179005,135.722644029799,135.821242154803,
135.91969993758,136.019922505352,136.11820206308,136.216448642154,136.314691725192,
136.416388913834,136.514773327253,136.618126903507,136.721480479761,136.820078604765,
136.918536387541,137.018758955314,137.117038513042,137.215285092116,137.313528175154,
137.415225363796,137.513609777215,137.616963353469,137.720316929723,137.818915054727,
137.917372837503,138.017595405276,138.115874963004,138.214121542077,138.312364625116,
138.414061813758,138.512446227176,138.61579980343,138.719153379684,138.8177616025,
138.916204188052,139.014551352321,139.112826031228,139.146050573222),
 .UNSPECIFIED.);
#1662=B_SPLINE_CURVE_WITH_KNOTS('',3,(#155703,#155704,#155705,#155706,#155707,
#155708,#155709,#155710,#155711,#155712,#155713,#155714,#155715,#155716,
#155717,#155718,#155719,#155720,#155721,#155722,#155723,#155724,#155725,
#155726,#155727,#155728,#155729,#155730,#155731,#155732,#155733,#155734,
#155735,#155736,#155737,#155738,#155739,#155740,#155741,#155742,#155743,
#155744,#155745,#155746,#155747,#155748,#155749,#155750,#155751,#155752,
#155753,#155754,#155755,#155756,#155757,#155758,#155759,#155760,#155761,
#155762,#155763,#155764,#155765,#155766,#155767,#155768,#155769,#155770,
#155771,#155772),.UNSPECIFIED.,.F.,.F.,(4,3,3,3,3,3,3,3,3,3,3,3,3,3,3,3,
3,3,3,3,3,3,3,4),(132.863178333069,132.961590250635,133.059905656005,133.158169527358,
133.256411368768,133.354660655115,133.453012760686,133.551418046858,133.649994520245,
133.724971129875,133.823569254879,133.922027037655,134.022249605428,134.120529163156,
134.218775742229,134.317018825268,134.41871601391,134.517100427329,134.620454003583,
134.723807579837,134.836338520701,134.948409000642,135.059693750752,135.088484104126),
 .UNSPECIFIED.);
#1663=B_SPLINE_CURVE_WITH_KNOTS('',3,(#155774,#155775,#155776,#155777,#155778,
#155779,#155780,#155781,#155782,#155783,#155784,#155785,#155786,#155787,
#155788,#155789,#155790,#155791,#155792,#155793,#155794,#155795,#155796,
#155797,#155798,#155799,#155800,#155801,#155802,#155803,#155804,#155805,
#155806,#155807,#155808,#155809,#155810,#155811,#155812,#155813,#155814,
#155815,#155816,#155817,#155818,#155819,#155820,#155821,#155822,#155823,
#155824,#155825,#155826,#155827,#155828,#155829,#155830,#155831,#155832,
#155833,#155834,#155835,#155836,#155837,#155838,#155839,#155840,#155841,
#155842,#155843),.UNSPECIFIED.,.F.,.F.,(4,3,3,3,3,3,3,3,3,3,3,3,3,3,3,3,
3,3,3,3,3,3,3,4),(132.86234124739,132.961797034881,133.060185441341,133.160174919349,
133.260164397356,133.35876252236,133.457220305136,133.557442872909,133.655722430637,
133.75396900971,133.852212092749,133.953909281391,134.05229369481,134.155647271063,
134.259000847317,134.356128675186,134.453094160804,134.549968416923,134.646782617699,
134.743567858738,134.84039997176,134.937256811786,135.034231214225,135.088484104361),
 .UNSPECIFIED.);
#1664=B_SPLINE_CURVE_WITH_KNOTS('',3,(#155844,#155845,#155846,#155847,#155848,
#155849,#155850,#155851),.UNSPECIFIED.,.F.,.F.,(4,1,1,1,1,4),(135.088484104361,
135.257837297279,136.256673747241,137.255510197203,138.254346647165,139.145213350467),
 .UNSPECIFIED.);
#1665=B_SPLINE_CURVE_WITH_KNOTS('',3,(#155857,#155858,#155859,#155860,#155861,
#155862,#155863,#155864,#155865,#155866,#155867,#155868,#155869,#155870,
#155871,#155872,#155873,#155874,#155875,#155876,#155877,#155878,#155879,
#155880,#155881,#155882,#155883,#155884,#155885,#155886,#155887,#155888,
#155889,#155890,#155891,#155892,#155893,#155894,#155895,#155896,#155897,
#155898,#155899,#155900,#155901,#155902,#155903,#155904,#155905,#155906,
#155907,#155908,#155909,#155910,#155911,#155912,#155913,#155914,#155915,
#155916,#155917,#155918,#155919,#155920,#155921,#155922,#155923,#155924,
#155925,#155926,#155927,#155928,#155929,#155930,#155931,#155932,#155933,
#155934,#155935,#155936,#155937,#155938,#155939,#155940,#155941,#155942,
#155943,#155944,#155945,#155946,#155947,#155948,#155949,#155950,#155951,
#155952,#155953,#155954,#155955,#155956,#155957,#155958,#155959,#155960,
#155961,#155962,#155963,#155964,#155965,#155966,#155967,#155968,#155969,
#155970,#155971,#155972,#155973,#155974,#155975,#155976,#155977,#155978,
#155979,#155980),.UNSPECIFIED.,.F.,.F.,(4,3,3,3,3,3,3,3,3,3,3,3,3,3,3,3,
3,3,3,3,3,3,3,3,3,3,3,3,3,3,3,3,3,3,3,3,3,3,3,3,3,4),(141.371669411768,
141.485016004535,141.600339367052,141.71566272957,141.814260854574,141.912718637351,
142.012941205123,142.111220762851,142.209467341925,142.307710424963,142.409407613606,
142.507792027024,142.611145603278,142.714499179532,142.813097304536,142.911555087312,
143.011777655085,143.110057212813,143.208303791887,143.306546874925,143.408244063567,
143.506628476986,143.60998205324,143.713335629494,143.811933754498,143.910391537274,
144.010614105047,144.108893662775,144.207140241849,144.305383324887,144.40708051353,
144.505464926948,144.608818503202,144.712172079456,144.810746601835,144.909191401425,
145.007536191867,145.105810582005,145.204060790384,145.302298022107,145.400579631044,
145.428467292648),.UNSPECIFIED.);
#1666=B_SPLINE_CURVE_WITH_KNOTS('',3,(#155981,#155982,#155983,#155984,#155985,
#155986,#155987,#155988,#155989,#155990,#155991,#155992,#155993,#155994,
#155995,#155996,#155997,#155998,#155999,#156000,#156001,#156002,#156003,
#156004,#156005,#156006,#156007,#156008,#156009,#156010,#156011,#156012,
#156013,#156014,#156015,#156016,#156017,#156018,#156019,#156020,#156021,
#156022,#156023,#156024,#156025,#156026,#156027,#156028,#156029,#156030,
#156031,#156032,#156033,#156034,#156035,#156036,#156037,#156038,#156039,
#156040,#156041,#156042,#156043,#156044,#156045,#156046,#156047,#156048,
#156049,#156050),.UNSPECIFIED.,.F.,.F.,(4,3,3,3,3,3,3,3,3,3,3,3,3,3,3,3,
3,3,3,3,3,3,3,4),(139.146050573222,139.244292836133,139.342541002963,139.440891057939,
139.539292908966,139.637867561271,139.717989829646,139.81658795465,139.915045737426,
140.015268305199,140.113547862927,140.211794442001,140.31003752504,140.411734713682,
140.510119127101,140.613472703354,140.716826279608,140.815569227393,140.914173010821,
141.012667061739,141.111081830931,141.209449097701,141.307822396311,141.371669411541),
 .UNSPECIFIED.);
#1667=B_SPLINE_CURVE_WITH_KNOTS('',3,(#156052,#156053,#156054,#156055,#156056,
#156057,#156058),.UNSPECIFIED.,.F.,.F.,(4,1,1,1,4),(139.145213350467,139.253183097127,
140.252019547089,141.250855997051,141.371669411541),.UNSPECIFIED.);
#1668=B_SPLINE_CURVE_WITH_KNOTS('',3,(#156059,#156060,#156061,#156062,#156063,
#156064,#156065,#156066,#156067,#156068,#156069,#156070,#156071,#156072,
#156073,#156074,#156075,#156076,#156077,#156078,#156079,#156080,#156081,
#156082,#156083,#156084,#156085,#156086,#156087,#156088,#156089,#156090,
#156091,#156092,#156093,#156094,#156095,#156096,#156097,#156098,#156099,
#156100,#156101,#156102,#156103,#156104,#156105,#156106,#156107,#156108,
#156109,#156110,#156111,#156112,#156113,#156114,#156115,#156116,#156117,
#156118,#156119,#156120,#156121,#156122,#156123,#156124,#156125,#156126,
#156127,#156128,#156129,#156130,#156131,#156132,#156133,#156134,#156135,
#156136,#156137,#156138,#156139,#156140,#156141,#156142,#156143,#156144,
#156145,#156146,#156147,#156148,#156149,#156150,#156151,#156152,#156153,
#156154,#156155,#156156,#156157,#156158,#156159,#156160,#156161,#156162,
#156163,#156164,#156165,#156166,#156167,#156168,#156169,#156170,#156171,
#156172,#156173,#156174,#156175,#156176,#156177,#156178,#156179,#156180,
#156181,#156182),.UNSPECIFIED.,.F.,.F.,(4,3,3,3,3,3,3,3,3,3,3,3,3,3,3,3,
3,3,3,3,3,3,3,3,3,3,3,3,3,3,3,3,3,3,3,3,3,3,3,3,3,4),(141.371669411541,
141.46883125416,141.566438903267,141.66339620349,141.760311911022,141.857216996242,
141.955335858935,142.052368429038,142.151030438025,142.249692447012,142.348290572016,
142.446748354793,142.546970922565,142.645250480293,142.743497059367,142.841740142405,
142.943437331048,143.041821744466,143.14517532072,143.248528896974,143.347127021978,
143.445584804754,143.545807372527,143.644086930255,143.742333509329,143.840576592367,
143.94227378101,144.040658194428,144.144011770682,144.247365346936,144.34596347194,
144.444421254716,144.544643822489,144.642923380217,144.741169959291,144.839413042329,
144.941110230971,145.03949464439,145.142848220644,145.246201796898,145.344774861169,
145.429604638483),.UNSPECIFIED.);
#1669=B_SPLINE_CURVE_WITH_KNOTS('',3,(#156188,#156189,#156190,#156191,#156192,
#156193,#156194,#156195,#156196),.UNSPECIFIED.,.F.,.F.,(4,1,1,1,1,1,4),
(147.65485471872,147.708681429341,148.707517879303,149.706354329265,150.705190779227,
151.704027229189,151.71225272303),.UNSPECIFIED.);
#1670=B_SPLINE_CURVE_WITH_KNOTS('',3,(#156197,#156198,#156199,#156200,#156201,
#156202,#156203,#156204,#156205,#156206,#156207,#156208,#156209,#156210,
#156211,#156212,#156213,#156214,#156215,#156216,#156217,#156218,#156219,
#156220,#156221,#156222,#156223,#156224,#156225,#156226,#156227,#156228,
#156229,#156230,#156231,#156232,#156233,#156234,#156235,#156236,#156237,
#156238,#156239,#156240,#156241,#156242,#156243,#156244,#156245,#156246,
#156247,#156248,#156249,#156250,#156251,#156252,#156253,#156254,#156255,
#156256,#156257,#156258,#156259,#156260,#156261,#156262,#156263,#156264,
#156265,#156266),.UNSPECIFIED.,.F.,.F.,(4,3,3,3,3,3,3,3,3,3,3,3,3,3,3,3,
3,3,3,3,3,3,3,4),(145.428467292648,145.52686558547,145.625438406774,145.711008529418,
145.809606654422,145.908064437198,146.008287004971,146.106566562699,146.204813141772,
146.303056224811,146.404753413453,146.503137826872,146.606491403125,146.709844979379,
146.807643480436,146.905302408374,147.002849316603,147.100335701354,147.197792033696,
147.295248746519,147.3927980835,147.490396206244,147.588155506493,147.65485471872),
 .UNSPECIFIED.);
#1671=B_SPLINE_CURVE_WITH_KNOTS('',3,(#156268,#156269,#156270,#156271,#156272,
#156273,#156274,#156275,#156276,#156277,#156278,#156279,#156280,#156281,
#156282,#156283,#156284,#156285,#156286,#156287,#156288,#156289,#156290,
#156291,#156292,#156293,#156294,#156295,#156296,#156297,#156298,#156299,
#156300,#156301,#156302,#156303,#156304,#156305,#156306,#156307,#156308,
#156309,#156310,#156311,#156312,#156313,#156314,#156315,#156316,#156317,
#156318,#156319,#156320,#156321,#156322,#156323,#156324,#156325,#156326,
#156327,#156328,#156329,#156330,#156331,#156332,#156333,#156334,#156335,
#156336,#156337),.UNSPECIFIED.,.F.,.F.,(4,3,3,3,3,3,3,3,3,3,3,3,3,3,3,3,
3,3,3,3,3,3,3,4),(145.429604638483,145.53153383953,145.629819415388,145.728068427782,
145.826310362661,145.924574690241,146.022950440083,146.121392805655,146.219991569703,
146.24503824686,146.343636371864,146.44209415464,146.542316722413,146.640596280141,
146.738842859215,146.837085942253,146.938783130895,147.037167544314,147.140521120568,
147.243874696822,147.352569174392,147.460952550046,147.568802109382,147.654854305383),
 .UNSPECIFIED.);
#1672=B_SPLINE_CURVE_WITH_KNOTS('',3,(#156338,#156339,#156340,#156341,#156342,
#156343,#156344,#156345),.UNSPECIFIED.,.F.,.F.,(4,1,1,1,1,4),(147.65485471872,
148.242711146784,149.241547596746,150.240384046707,151.239220496669,151.712342645016),
 .UNSPECIFIED.);
#1673=B_SPLINE_CURVE_WITH_KNOTS('',3,(#156351,#156352,#156353,#156354,#156355,
#156356,#156357,#156358,#156359,#156360,#156361,#156362,#156363,#156364,
#156365,#156366,#156367,#156368,#156369,#156370,#156371,#156372,#156373,
#156374,#156375,#156376,#156377,#156378,#156379,#156380,#156381,#156382,
#156383,#156384,#156385,#156386,#156387,#156388,#156389,#156390,#156391,
#156392,#156393,#156394,#156395,#156396,#156397,#156398,#156399,#156400,
#156401,#156402,#156403,#156404,#156405,#156406,#156407,#156408,#156409,
#156410,#156411,#156412,#156413,#156414,#156415,#156416,#156417,#156418,
#156419,#156420,#156421,#156422,#156423,#156424,#156425,#156426,#156427,
#156428,#156429,#156430,#156431,#156432,#156433,#156434,#156435,#156436,
#156437,#156438,#156439,#156440,#156441,#156442,#156443,#156444,#156445,
#156446,#156447,#156448,#156449,#156450,#156451,#156452,#156453,#156454,
#156455,#156456,#156457,#156458,#156459,#156460,#156461,#156462,#156463,
#156464,#156465,#156466,#156467,#156468,#156469,#156470,#156471,#156472,
#156473,#156474),.UNSPECIFIED.,.F.,.F.,(4,3,3,3,3,3,3,3,3,3,3,3,3,3,3,3,
3,3,3,3,3,3,3,3,3,3,3,3,3,3,3,3,3,3,3,3,3,3,3,3,3,4),(153.9380400259,154.035163898234,
154.132222574362,154.229246955324,154.326267897773,154.423381488606,154.520541056366,
154.617870832504,154.700536579074,154.799134704076,154.897592486852,154.997815054625,
155.096094612352,155.194341191424,155.292584274461,155.394281463105,155.492665876523,
155.596019452779,155.699373029036,155.797971154037,155.896428936811,155.996651504585,
156.09493106231,156.193177641381,156.291420724417,156.393117913062,156.491502326478,
156.594855902738,156.698209478998,156.796807604012,156.895265386799,156.995487954569,
157.093767512308,157.192014091391,157.29025717444,157.39195436307,157.490338776499,
157.593692352729,157.69704592896,157.795632129861,157.89577059138,157.995909052899),
 .UNSPECIFIED.);
#1674=B_SPLINE_CURVE_WITH_KNOTS('',3,(#156475,#156476,#156477,#156478,#156479,
#156480),.UNSPECIFIED.,.F.,.F.,(4,1,1,4),(151.71225272303,152.702863679151,
153.701700129113,153.938039726484),.UNSPECIFIED.);
#1675=B_SPLINE_CURVE_WITH_KNOTS('',3,(#156482,#156483,#156484,#156485,#156486,
#156487),.UNSPECIFIED.,.F.,.F.,(4,1,1,4),(151.712342645016,152.238056946631,
153.236893396593,153.9380400259),.UNSPECIFIED.);
#1676=B_SPLINE_CURVE_WITH_KNOTS('',3,(#156488,#156489,#156490,#156491,#156492,
#156493,#156494,#156495,#156496,#156497,#156498,#156499,#156500,#156501,
#156502,#156503,#156504,#156505,#156506,#156507,#156508,#156509,#156510,
#156511,#156512,#156513,#156514,#156515,#156516,#156517,#156518,#156519,
#156520,#156521,#156522,#156523,#156524,#156525,#156526,#156527,#156528,
#156529,#156530,#156531,#156532,#156533,#156534,#156535,#156536,#156537,
#156538,#156539,#156540,#156541,#156542,#156543,#156544,#156545,#156546,
#156547,#156548,#156549,#156550,#156551,#156552,#156553,#156554,#156555,
#156556,#156557,#156558,#156559,#156560,#156561,#156562,#156563,#156564,
#156565,#156566,#156567,#156568,#156569,#156570,#156571,#156572,#156573,
#156574,#156575,#156576,#156577,#156578,#156579,#156580,#156581,#156582,
#156583,#156584,#156585,#156586,#156587,#156588,#156589,#156590,#156591,
#156592,#156593,#156594,#156595,#156596,#156597,#156598,#156599,#156600,
#156601,#156602,#156603,#156604,#156605,#156606,#156607,#156608,#156609,
#156610,#156611),.UNSPECIFIED.,.F.,.F.,(4,3,3,3,3,3,3,3,3,3,3,3,3,3,3,3,
3,3,3,3,3,3,3,3,3,3,3,3,3,3,3,3,3,3,3,3,3,3,3,3,3,4),(153.938040202782,
154.056659980249,154.176963651006,154.235729846555,154.334327971559,154.432785754335,
154.533008322108,154.631287879836,154.729534458909,154.827777541948,154.92947473059,
155.027859144009,155.131212720263,155.234566296517,155.33316442152,155.431622204297,
155.531844772069,155.630124329797,155.72837090887,155.826613991908,155.928311180551,
156.026695593969,156.130049170224,156.233402746479,156.332000871484,156.430458654262,
156.530681222035,156.628960779764,156.727207358839,156.825450441879,156.927147630519,
157.02553204394,157.12888562019,157.232239196441,157.330809964386,157.429252216966,
157.527595662276,157.625869905311,157.724128943529,157.822375482199,157.920688283555,
157.994793997602),.UNSPECIFIED.);
#1677=B_SPLINE_CURVE_WITH_KNOTS('',3,(#156617,#156618,#156619,#156620,#156621,
#156622,#156623,#156624),.UNSPECIFIED.,.F.,.F.,(4,1,1,1,1,4),(160.221227414851,
160.693555278846,161.692391728808,162.691228178769,163.690064628731,164.278110045036),
 .UNSPECIFIED.);
#1678=B_SPLINE_CURVE_WITH_KNOTS('',3,(#156625,#156626,#156627,#156628,#156629,
#156630,#156631,#156632,#156633,#156634,#156635,#156636,#156637,#156638,
#156639,#156640,#156641,#156642,#156643,#156644,#156645,#156646,#156647,
#156648,#156649,#156650,#156651,#156652,#156653,#156654,#156655,#156656,
#156657,#156658,#156659,#156660,#156661,#156662,#156663,#156664,#156665,
#156666,#156667,#156668,#156669,#156670,#156671,#156672,#156673,#156674,
#156675,#156676,#156677,#156678,#156679,#156680,#156681,#156682,#156683,
#156684,#156685,#156686,#156687,#156688,#156689,#156690,#156691,#156692,
#156693,#156694),.UNSPECIFIED.,.F.,.F.,(4,3,3,3,3,3,3,3,3,3,3,3,3,3,3,3,
3,3,3,3,3,3,3,4),(157.995909052899,158.094187845048,158.192434134029,158.290677402052,
158.39197864627,158.490363756051,158.593123067487,158.695882378922,158.794480503912,
158.892938286674,158.993160854451,159.091440412165,159.189686991223,159.287930074248,
159.389627262907,159.488011676311,159.591365252598,159.694718828884,159.797216560019,
159.903218753284,160.005303397592,160.107256278838,160.209067828957,160.22122533308),
 .UNSPECIFIED.);
#1679=B_SPLINE_CURVE_WITH_KNOTS('',3,(#156696,#156697,#156698,#156699,#156700,
#156701,#156702,#156703,#156704,#156705,#156706,#156707,#156708,#156709,
#156710,#156711,#156712,#156713,#156714,#156715,#156716,#156717,#156718,
#156719,#156720,#156721,#156722,#156723,#156724,#156725,#156726,#156727,
#156728,#156729,#156730,#156731,#156732,#156733,#156734,#156735,#156736,
#156737,#156738,#156739,#156740,#156741,#156742,#156743,#156744,#156745,
#156746,#156747,#156748,#156749,#156750,#156751,#156752,#156753,#156754,
#156755,#156756,#156757,#156758,#156759,#156760,#156761,#156762,#156763,
#156764,#156765),.UNSPECIFIED.,.F.,.F.,(4,3,3,3,3,3,3,3,3,3,3,3,3,3,3,3,
3,3,3,3,3,3,3,4),(157.994793997602,158.093225117261,158.191816683924,158.231075646402,
158.329673771403,158.428131554177,158.52835412195,158.626633679676,158.724880258747,
158.823123341782,158.924820530428,159.023204943844,159.126558520104,159.229912096364,
159.328378576654,159.426704810661,159.526019875932,159.624169149678,159.722285836342,
159.820399593048,159.920606027993,160.018861091251,160.120043212039,160.221225332828),
 .UNSPECIFIED.);
#1680=B_SPLINE_CURVE_WITH_KNOTS('',3,(#156766,#156767,#156768,#156769,#156770,
#156771,#156772,#156773,#156774,#156775,#156776,#156777,#156778,#156779,
#156780,#156781,#156782,#156783,#156784,#156785,#156786,#156787,#156788,
#156789,#156790,#156791,#156792,#156793,#156794,#156795,#156796,#156797,
#156798,#156799,#156800,#156801,#156802,#156803,#156804,#156805,#156806,
#156807,#156808,#156809,#156810,#156811,#156812,#156813,#156814,#156815,
#156816,#156817,#156818,#156819,#156820,#156821,#156822,#156823,#156824,
#156825,#156826,#156827,#156828,#156829,#156830,#156831,#156832,#156833,
#156834,#156835,#156836,#156837,#156838,#156839,#156840,#156841,#156842,
#156843,#156844,#156845,#156846,#156847,#156848,#156849,#156850,#156851,
#156852,#156853,#156854,#156855,#156856,#156857,#156858,#156859,#156860,
#156861,#156862,#156863,#156864,#156865,#156866,#156867,#156868,#156869,
#156870,#156871,#156872,#156873,#156874,#156875,#156876,#156877,#156878,
#156879,#156880,#156881,#156882,#156883,#156884,#156885,#156886,#156887,
#156888,#156889,#156890,#156891,#156892),.UNSPECIFIED.,.F.,.F.,(4,3,3,3,
3,3,3,3,3,3,3,3,3,3,3,3,3,3,3,3,3,3,3,3,3,3,3,3,3,3,3,3,3,3,3,3,3,3,3,3,
3,3,4),(160.22122533308,160.228748546326,160.327346671318,160.425804454083,
160.526027021859,160.624306579575,160.722553158637,160.820796241664,160.92249343032,
161.020877843728,161.124231420008,161.227584996288,161.326183121278,161.424640904041,
161.524863471817,161.623143029531,161.72138960859,161.819632691614,161.921329880273,
162.019714293677,162.123067869964,162.22642144625,162.325019571326,162.423477354176,
162.52369992193,162.621979479731,162.720226058877,162.818469141987,162.920166330544,
163.018550744033,163.121904320123,163.225257896212,163.323856021116,163.422313803792,
163.52253637159,163.62081592922,163.719062508196,163.817305591137,163.919002779896,
164.017387193222,164.120740769698,164.224094346174,164.278857710125),
 .UNSPECIFIED.);
#1681=B_SPLINE_CURVE_WITH_KNOTS('',3,(#156898,#156899,#156900,#156901,#156902,
#156903,#156904,#156905,#156906,#156907,#156908,#156909,#156910,#156911,
#156912,#156913,#156914,#156915,#156916,#156917,#156918,#156919,#156920,
#156921,#156922,#156923,#156924,#156925,#156926,#156927,#156928,#156929,
#156930,#156931,#156932,#156933,#156934,#156935,#156936,#156937,#156938,
#156939,#156940,#156941,#156942,#156943,#156944,#156945,#156946,#156947,
#156948,#156949,#156950,#156951,#156952,#156953,#156954,#156955,#156956,
#156957,#156958,#156959,#156960,#156961,#156962,#156963,#156964,#156965,
#156966,#156967,#156968,#156969,#156970,#156971,#156972,#156973,#156974,
#156975,#156976,#156977,#156978,#156979,#156980,#156981,#156982,#156983,
#156984,#156985,#156986,#156987,#156988,#156989,#156990,#156991,#156992,
#156993,#156994,#156995,#156996,#156997,#156998,#156999,#157000,#157001,
#157002,#157003,#157004,#157005,#157006,#157007,#157008,#157009,#157010,
#157011,#157012,#157013,#157014,#157015,#157016,#157017,#157018,#157019,
#157020,#157021),.UNSPECIFIED.,.F.,.F.,(4,3,3,3,3,3,3,3,3,3,3,3,3,3,3,3,
3,3,3,3,3,3,3,3,3,3,3,3,3,3,3,3,3,3,3,3,3,3,3,3,3,4),(166.504410640259,
166.65291077017,166.686573978617,166.785172097224,166.883629873609,166.983852442981,
167.082131994377,167.180378567154,167.278621643939,167.380318840099,167.478703247436,
167.582056838008,167.685410428579,167.784008554555,167.882466338245,167.982688905782,
168.080968464275,168.179215044057,168.277458127747,168.379155315446,168.477539729369,
168.580893303955,168.684246878541,168.782845025265,168.881302829864,168.981525392194,
169.079804971833,169.178051572804,169.276294677697,169.377991840398,169.476376275343,
169.579729801923,169.683083328503,169.781689728,169.880127484756,169.978469449952,
170.076745220109,170.174984321157,170.273261950328,170.371554712907,170.469968413916,
170.561255386023),.UNSPECIFIED.);
#1682=B_SPLINE_CURVE_WITH_KNOTS('',3,(#157022,#157023,#157024,#157025,#157026,
#157027),.UNSPECIFIED.,.F.,.F.,(4,1,1,4),(164.278110045036,164.688901078693,
165.687737528655,166.504405683028),.UNSPECIFIED.);
#1683=B_SPLINE_CURVE_WITH_KNOTS('',3,(#157029,#157030,#157031,#157032,#157033,
#157034,#157035,#157036,#157037,#157038,#157039,#157040,#157041,#157042,
#157043,#157044,#157045,#157046,#157047,#157048,#157049,#157050,#157051,
#157052,#157053,#157054,#157055,#157056,#157057,#157058,#157059,#157060,
#157061,#157062,#157063,#157064,#157065,#157066,#157067,#157068,#157069,
#157070,#157071,#157072,#157073,#157074,#157075,#157076,#157077,#157078,
#157079,#157080,#157081,#157082,#157083,#157084,#157085,#157086,#157087,
#157088,#157089,#157090,#157091,#157092,#157093,#157094,#157095,#157096,
#157097,#157098),.UNSPECIFIED.,.F.,.F.,(4,3,3,3,3,3,3,3,3,3,3,3,3,3,3,3,
3,3,3,3,3,3,3,4),(164.278857710125,164.377373851694,164.475767893135,164.574072766376,
164.672330974244,164.770572014167,164.868825358762,164.967184404754,165.065600998296,
165.164183798452,165.222930796136,165.321528921637,165.419986704913,165.520209272561,
165.618488830789,165.71673541036,165.814978493895,165.916675681946,166.015060095852,
166.118413670974,166.221767246097,166.344599874398,166.465474953135,166.504410639987),
 .UNSPECIFIED.);
#1684=B_SPLINE_CURVE_WITH_KNOTS('',3,(#157099,#157100,#157101,#157102,#157103,
#157104,#157105,#157106,#157107,#157108,#157109,#157110,#157111,#157112,
#157113,#157114,#157115,#157116,#157117,#157118,#157119,#157120,#157121,
#157122,#157123,#157124,#157125,#157126,#157127,#157128,#157129,#157130,
#157131,#157132,#157133,#157134,#157135,#157136,#157137,#157138,#157139,
#157140,#157141,#157142,#157143,#157144,#157145,#157146,#157147,#157148,
#157149,#157150,#157151,#157152,#157153,#157154,#157155,#157156,#157157,
#157158,#157159,#157160,#157161,#157162,#157163,#157164,#157165,#157166,
#157167,#157168,#157169,#157170,#157171,#157172,#157173,#157174,#157175,
#157176,#157177,#157178,#157179,#157180,#157181,#157182,#157183,#157184,
#157185,#157186,#157187,#157188,#157189,#157190,#157191,#157192,#157193,
#157194,#157195,#157196,#157197,#157198,#157199,#157200,#157201,#157202,
#157203,#157204,#157205,#157206,#157207,#157208,#157209,#157210,#157211,
#157212,#157213,#157214,#157215,#157216,#157217,#157218,#157219,#157220,
#157221,#157222,#157223,#157224,#157225),.UNSPECIFIED.,.F.,.F.,(4,3,3,3,
3,3,3,3,3,3,3,3,3,3,3,3,3,3,3,3,3,3,3,3,3,3,3,3,3,3,3,3,3,3,3,3,3,3,3,3,
3,3,4),(166.504410640259,166.601913126298,166.699371433805,166.796815990355,
166.894277201717,166.99184617322,167.089478292227,167.187269535427,167.220603696059,
167.319201820913,167.417659603532,167.517882171343,167.616161728894,167.714408307783,
167.81265139063,167.914348579478,168.012732992691,168.116086569356,168.219440146021,
168.318038274359,168.416496060482,168.516718627419,168.614998188501,168.713244770923,
168.811487857301,168.913185041971,169.011569458673,169.114923027328,169.218276595983,
169.316874714587,169.41533249097,169.515555060342,169.613834611735,169.71208118451,
169.810324261293,169.912021457456,170.010405864791,170.113759455368,170.217113045945,
170.315689889892,170.414143809247,170.512486666546,170.562190622809),
 .UNSPECIFIED.);
#1685=B_SPLINE_CURVE_WITH_KNOTS('',3,(#157231,#157232,#157233,#157234,#157235,
#157236,#157237,#157238,#157239,#157240,#157241,#157242,#157243,#157244,
#157245,#157246,#157247,#157248,#157249,#157250,#157251,#157252,#157253,
#157254,#157255,#157256,#157257,#157258,#157259,#157260,#157261,#157262,
#157263,#157264,#157265,#157266,#157267,#157268,#157269,#157270,#157271,
#157272,#157273,#157274,#157275,#157276,#157277,#157278,#157279,#157280,
#157281,#157282,#157283,#157284,#157285,#157286,#157287,#157288,#157289,
#157290,#157291,#157292,#157293,#157294,#157295,#157296,#157297,#157298,
#157299,#157300,#157301,#157302,#157303,#157304,#157305,#157306,#157307,
#157308,#157309,#157310,#157311,#157312,#157313,#157314,#157315,#157316,
#157317,#157318,#157319,#157320,#157321,#157322,#157323,#157324,#157325,
#157326,#157327,#157328,#157329,#157330,#157331,#157332,#157333,#157334,
#157335,#157336,#157337,#157338,#157339,#157340,#157341,#157342,#157343,
#157344,#157345,#157346,#157347,#157348,#157349,#157350,#157351,#157352,
#157353,#157354,#157355,#157356,#157357),.UNSPECIFIED.,.F.,.F.,(4,3,3,3,
3,3,3,3,3,3,3,3,3,3,3,3,3,3,3,3,3,3,3,3,3,3,3,3,3,3,3,3,3,3,3,3,3,3,3,3,
3,3,4),(172.787595947668,172.884841558898,172.98404000508,173.081071837534,
173.178059269357,173.275033213409,173.375882192145,173.472980625916,173.570144969666,
173.667458407301,173.67842912835,173.777027506426,173.875485539767,173.975708044585,
174.073987845019,174.172234663368,174.270477981962,174.372174881049,174.470559518455,
174.573912548384,174.677265578312,174.775864530901,174.874323147236,174.974545507366,
175.072825907183,175.171073329681,175.269317256364,175.371013449341,175.469398698301,
175.572750363288,175.676102028274,175.774697487766,175.873152601892,175.973375836435,
176.07165273689,176.169896668633,176.268137117691,176.369837457827,176.468219297092,
176.571578887664,176.674938478236,176.773518527172,176.845520716454),
 .UNSPECIFIED.);
#1686=B_SPLINE_CURVE_WITH_KNOTS('',3,(#157358,#157359,#157360,#157361,#157362,
#157363,#157364,#157365,#157366,#157367,#157368,#157369,#157370,#157371,
#157372,#157373,#157374,#157375,#157376,#157377,#157378,#157379,#157380,
#157381,#157382,#157383,#157384,#157385,#157386,#157387,#157388,#157389,
#157390,#157391,#157392,#157393,#157394,#157395,#157396,#157397,#157398,
#157399,#157400,#157401,#157402,#157403,#157404,#157405,#157406,#157407,
#157408,#157409,#157410,#157411,#157412,#157413,#157414,#157415,#157416,
#157417,#157418,#157419,#157420,#157421,#157422,#157423,#157424,#157425,
#157426,#157427),.UNSPECIFIED.,.F.,.F.,(4,3,3,3,3,3,3,3,3,3,3,3,3,3,3,3,
3,3,3,3,3,3,3,4),(170.561255386023,170.659855701315,170.681919778464,170.780517924859,
170.878975728637,170.979198291111,171.07747786875,171.175724467288,171.273967569322,
171.375664734098,171.474049165163,171.577402696795,171.680756228426,171.7793544904,
171.877812410935,171.978034944366,172.07631464078,172.174561358581,172.272804580209,
172.374501604754,172.472886155,172.576239416694,172.679592678388,172.787595947439),
 .UNSPECIFIED.);
#1687=B_SPLINE_CURVE_WITH_KNOTS('',3,(#157429,#157430,#157431,#157432,#157433,
#157434,#157435,#157436,#157437,#157438,#157439,#157440,#157441,#157442,
#157443,#157444,#157445,#157446,#157447,#157448,#157449,#157450,#157451,
#157452,#157453,#157454,#157455,#157456,#157457,#157458,#157459,#157460,
#157461,#157462,#157463,#157464,#157465,#157466,#157467,#157468,#157469,
#157470,#157471,#157472,#157473,#157474,#157475,#157476,#157477,#157478,
#157479,#157480,#157481,#157482,#157483,#157484,#157485,#157486,#157487,
#157488,#157489,#157490,#157491,#157492,#157493,#157494,#157495,#157496,
#157497,#157498),.UNSPECIFIED.,.F.,.F.,(4,3,3,3,3,3,3,3,3,3,3,3,3,3,3,3,
3,3,3,3,3,3,3,4),(170.562190622809,170.660450459433,170.758691657909,170.85694369146,
170.955300563434,171.053713662279,171.152294456207,171.215949495907,171.314547642641,
171.413005447249,171.513228009576,171.611507589225,171.709754190205,171.807997295108,
171.909694457798,172.008078892752,172.11143241931,172.214785945869,172.315617765141,
172.416285943305,172.516781875028,172.617176498107,172.717484579422,172.787595947439),
 .UNSPECIFIED.);
#1688=B_SPLINE_CURVE_WITH_KNOTS('',3,(#157499,#157500,#157501,#157502,#157503,
#157504,#157505,#157506),.UNSPECIFIED.,.F.,.F.,(4,1,1,1,1,4),(172.787601414895,
173.21362239583,174.212458845792,175.211295295754,176.210131745716,176.84428202222),
 .UNSPECIFIED.);
#1689=B_SPLINE_CURVE_WITH_KNOTS('',3,(#157512,#157513,#157514,#157515,#157516,
#157517,#157518,#157519),.UNSPECIFIED.,.F.,.F.,(4,1,1,1,1,4),(179.070781254618,
179.671447828121,180.670284278083,181.669120728045,182.667957178007,183.128402505335),
 .UNSPECIFIED.);
#1690=B_SPLINE_CURVE_WITH_KNOTS('',3,(#157520,#157521,#157522,#157523,#157524,
#157525,#157526,#157527,#157528,#157529,#157530,#157531,#157532,#157533,
#157534,#157535,#157536,#157537,#157538,#157539,#157540,#157541,#157542,
#157543,#157544,#157545,#157546,#157547,#157548,#157549,#157550,#157551,
#157552,#157553,#157554,#157555,#157556,#157557,#157558,#157559,#157560,
#157561,#157562,#157563,#157564,#157565,#157566,#157567,#157568,#157569,
#157570,#157571,#157572,#157573,#157574,#157575,#157576,#157577,#157578,
#157579,#157580,#157581,#157582,#157583,#157584,#157585,#157586,#157587,
#157588,#157589),.UNSPECIFIED.,.F.,.F.,(4,3,3,3,3,3,3,3,3,3,3,3,3,3,3,3,
3,3,3,3,3,3,3,4),(176.845520716454,176.949052492922,177.047346541156,177.145600633247,
177.243844255663,177.342106876084,177.440478991019,177.538914666061,177.637509863883,
177.673774928198,177.772377760441,177.870840294725,177.971061680154,178.069346062747,
178.167597483387,178.265845418215,178.367536908201,178.465926148849,178.569268763504,
178.672611378159,178.782250126366,178.891545491967,179.000249383586,179.070781030157),
 .UNSPECIFIED.);
#1691=B_SPLINE_CURVE_WITH_KNOTS('',3,(#157591,#157592,#157593,#157594,#157595,
#157596),.UNSPECIFIED.,.F.,.F.,(4,1,1,4),(176.84428202222,177.208968195678,
178.20780464564,179.070781254618),.UNSPECIFIED.);
#1692=B_SPLINE_CURVE_WITH_KNOTS('',3,(#157597,#157598,#157599,#157600,#157601,
#157602,#157603,#157604),.UNSPECIFIED.,.F.,.F.,(4,1,1,1,1,4),(179.070781254618,
179.206641095602,180.205477545564,181.204313995525,182.203150445487,183.127688252684),
 .UNSPECIFIED.);
#1693=B_SPLINE_CURVE_WITH_KNOTS('',3,(#157610,#157611,#157612,#157613,#157614,
#157615,#157616,#157617,#157618,#157619,#157620,#157621,#157622,#157623,
#157624,#157625),.UNSPECIFIED.,.F.,.F.,(4,2,2,2,2,2,2,4),(-3.36796875566957,
-3.29693602662566,-3.22761043814152,-3.1044360662705,-3.02217397688405,
-2.85177102547367,-2.77989462151021,-2.68789784099922),.UNSPECIFIED.);
#1694=B_SPLINE_CURVE_WITH_KNOTS('',3,(#157631,#157632,#157633,#157634,#157635,
#157636,#157637,#157638,#157639,#157640,#157641,#157642,#157643,#157644,
#157645,#157646,#157647,#157648,#157649,#157650,#157651,#157652,#157653,
#157654,#157655,#157656,#157657,#157658,#157659,#157660,#157661,#157662,
#157663,#157664,#157665,#157666,#157667,#157668,#157669,#157670,#157671,
#157672,#157673,#157674,#157675,#157676,#157677,#157678,#157679,#157680,
#157681,#157682,#157683,#157684),.UNSPECIFIED.,.F.,.F.,(4,2,2,2,2,2,2,2,
2,2,2,2,2,2,2,2,2,2,2,2,2,2,2,2,2,2,4),(-2.68789784099922,-2.65408837964258,
-2.57621411781424,-2.4966237333734,-2.32905307278914,-2.2450929033377,-2.17225677845503,
-2.05508950305336,-1.97375003241058,-1.85231723560798,-1.68441649845486,
-1.51608522360846,-1.44252219577298,-1.30207940119469,-1.21379664641263,
-1.12981832981553,-0.980005758162937,-0.912771512159761,-0.811790608062358,
-0.6822244712479,-0.609196859613438,-0.468499066483631,-0.385607510180293,
-0.301727696250491,-0.150758602094993,-0.0760649568285229,-0.000831943578446319),
 .UNSPECIFIED.);
#1695=B_SPLINE_CURVE_WITH_KNOTS('',3,(#157687,#157688,#157689,#157690,#157691,
#157692,#157693,#157694,#157695,#157696,#157697,#157698,#157699,#157700,
#157701,#157702,#157703,#157704,#157705,#157706,#157707,#157708,#157709,
#157710,#157711,#157712,#157713,#157714,#157715,#157716,#157717,#157718,
#157719,#157720,#157721,#157722,#157723,#157724,#157725,#157726,#157727,
#157728,#157729,#157730,#157731,#157732,#157733,#157734,#157735,#157736,
#157737,#157738),.UNSPECIFIED.,.F.,.F.,(4,2,2,2,2,2,2,2,2,2,2,2,2,2,2,2,
2,2,2,2,2,2,2,2,2,4),(2.08290412127981E-5,0.148616879989859,0.210346499036526,
0.277678159472066,0.445327467469216,0.529291339569611,0.612068174123259,
0.726650632271939,0.806873057478271,0.925431469321915,1.00702977628667,
1.12919268297785,1.21136628889785,1.38178661778949,1.45314215401029,1.57770656729397,
1.65588321631932,1.73550058497634,1.9026016001689,1.98657761141511,2.07050498841144,
2.21332407327658,2.28618427846037,2.41365321730892,2.49217571148828,2.63428973736591),
 .UNSPECIFIED.);
#1696=B_SPLINE_CURVE_WITH_KNOTS('',3,(#157743,#157744,#157745,#157746,#157747,
#157748,#157749,#157750,#157751,#157752,#157753,#157754,#157755,#157756,
#157757,#157758,#157759,#157760,#157761,#157762,#157763,#157764,#157765,
#157766,#157767,#157768,#157769,#157770,#157771,#157772,#157773,#157774,
#157775,#157776,#157777,#157778,#157779,#157780,#157781,#157782,#157783,
#157784,#157785,#157786,#157787,#157788,#157789,#157790,#157791,#157792,
#157793,#157794,#157795,#157796,#157797,#157798,#157799,#157800,#157801,
#157802,#157803,#157804,#157805,#157806,#157807,#157808,#157809,#157810,
#157811,#157812,#157813,#157814,#157815,#157816,#157817,#157818,#157819,
#157820,#157821,#157822,#157823,#157824,#157825,#157826,#157827,#157828,
#157829,#157830,#157831,#157832,#157833,#157834,#157835,#157836,#157837,
#157838,#157839,#157840,#157841,#157842,#157843,#157844,#157845,#157846,
#157847,#157848,#157849,#157850,#157851,#157852,#157853,#157854,#157855,
#157856,#157857,#157858,#157859,#157860,#157861,#157862,#157863,#157864,
#157865,#157866,#157867,#157868,#157869,#157870,#157871,#157872,#157873,
#157874,#157875,#157876,#157877,#157878,#157879,#157880,#157881,#157882,
#157883,#157884,#157885,#157886,#157887,#157888,#157889,#157890,#157891,
#157892,#157893,#157894,#157895,#157896,#157897,#157898,#157899,#157900,
#157901,#157902,#157903,#157904,#157905,#157906,#157907,#157908,#157909,
#157910,#157911,#157912,#157913,#157914,#157915,#157916,#157917,#157918,
#157919,#157920,#157921,#157922,#157923,#157924,#157925,#157926,#157927,
#157928,#157929,#157930,#157931,#157932,#157933,#157934,#157935,#157936,
#157937,#157938,#157939,#157940,#157941,#157942,#157943,#157944,#157945,
#157946,#157947,#157948,#157949,#157950,#157951,#157952,#157953,#157954,
#157955,#157956,#157957,#157958,#157959,#157960,#157961,#157962),
 .UNSPECIFIED.,.F.,.F.,(4,3,3,3,3,3,3,3,3,3,3,3,3,3,3,3,3,3,3,3,3,3,3,3,
3,3,3,3,3,3,3,3,3,3,3,3,3,3,3,3,3,3,3,3,3,3,3,3,3,3,3,3,3,3,3,3,3,3,3,3,
3,3,3,3,3,3,3,3,3,3,3,3,3,4),(-16.4213910178811,-16.3286432460334,-16.2359126775523,
-16.1431937736906,-16.0824674261131,-15.9941326347525,-15.9058201280992,
-15.81748971347,-15.7291508902718,-15.6407545361228,-15.5951199283521,-15.4994686331016,
-15.401544582474,-15.3059685045778,-15.2068704675844,-15.1077724305911,
-15.0193184286812,-14.9308670580831,-14.8423692825813,-14.7538469094734,
-14.6652436972666,-14.6204249328301,-14.5321659959703,-14.4439802741915,
-14.3558480516816,-14.2670832873849,-14.1789810556079,-14.0908703594027,
-14.0027333871464,-13.9134825246869,-13.8251922454331,-13.7354610913706,
-13.6457299373081,-13.5603980691463,-13.4751819518284,-13.3900578392207,
-13.3050021057494,-13.2199819233987,-13.134977242644,-13.0499668163815,
-12.9649293941461,-12.8797915746879,-12.7945965012499,-12.7092654850702,
-12.6710349417861,-12.5825725222911,-12.4942230261398,-12.405966583943,
-12.3172632542332,-12.2291343186378,-12.1410336270666,-12.0529433623445,
-11.9637925083244,-11.8756388741685,-11.7859894102163,-11.6963399462641,
-11.6077342332092,-11.5191955002859,-11.4307068279097,-11.342248612659,
-11.2537923358304,-11.2089924485031,-11.1135915257343,-11.0156048819863,
-10.9199968256523,-10.8208208881972,-10.7216449507421,-10.6332474245461,
-10.5448987428145,-10.4565720082927,-10.3682595889264,-10.2799238818341,
-10.2342974529811,-10.1382057107015),.UNSPECIFIED.);
#1697=B_SPLINE_CURVE_WITH_KNOTS('',3,(#157963,#157964,#157965,#157966,#157967,
#157968,#157969,#157970,#157971,#157972,#157973,#157974,#157975,#157976,
#157977,#157978,#157979,#157980,#157981,#157982,#157983,#157984,#157985,
#157986,#157987,#157988,#157989,#157990,#157991,#157992,#157993,#157994,
#157995,#157996,#157997,#157998,#157999,#158000,#158001,#158002,#158003,
#158004,#158005,#158006,#158007,#158008,#158009,#158010,#158011,#158012,
#158013,#158014,#158015,#158016,#158017,#158018,#158019,#158020,#158021,
#158022,#158023,#158024,#158025,#158026),.UNSPECIFIED.,.F.,.F.,(4,2,2,2,
2,2,2,2,2,2,2,2,2,2,2,2,2,2,2,2,2,2,2,2,2,2,2,2,2,2,2,4),(2.63428973736591,
2.66088030343492,2.74224037341081,2.8234354530902,2.94015318077752,3.00738558007736,
3.13228271568951,3.20336580092265,3.37373005819757,3.45586954025754,3.57847978926214,
3.66000380813647,3.77621516884977,3.85553026353794,3.97452927204004,4.0648220573991,
4.1729444122466,4.24437363486414,4.40914497732687,4.49070881257043,4.62100573148373,
4.68806932974065,4.80426761483173,4.96307722778861,4.99098169170844,5.01472046629936,
5.08915323440459,5.15916500631349,5.18798383976303,5.21418265554997,5.25339267367173,
5.32107893380752),.UNSPECIFIED.);
#1698=B_SPLINE_CURVE_WITH_KNOTS('',3,(#158031,#158032,#158033,#158034,#158035,
#158036,#158037,#158038,#158039,#158040,#158041,#158042,#158043,#158044,
#158045,#158046,#158047,#158048,#158049,#158050,#158051,#158052,#158053,
#158054,#158055,#158056,#158057,#158058,#158059,#158060,#158061,#158062,
#158063,#158064,#158065,#158066,#158067,#158068,#158069,#158070,#158071,
#158072,#158073,#158074,#158075,#158076,#158077,#158078,#158079,#158080,
#158081,#158082,#158083,#158084,#158085,#158086),.UNSPECIFIED.,.F.,.F.,
(4,2,2,2,2,2,2,2,2,2,2,2,2,2,2,2,2,2,2,2,2,2,2,2,2,2,2,4),(1.64869401953039,
1.65982716497674,1.79037275571469,1.89090356673503,1.95818813039972,2.0409203859265,
2.16786929391265,2.30166199712435,2.38022082935311,2.50764971042287,2.58040208492111,
2.72361472000731,2.80826242758488,2.89225516964731,3.05897279728656,3.13861342395075,
3.22546685407399,3.30946904726711,3.4761010374434,3.55574189436597,3.63441392828252,
3.75681848930802,3.82840234120101,3.99886928816814,4.08084321955354,4.19285213499667,
4.26394696517578,4.33610062123442),.UNSPECIFIED.);
#1699=B_SPLINE_CURVE_WITH_KNOTS('',3,(#158087,#158088,#158089,#158090,#158091,
#158092,#158093,#158094,#158095,#158096,#158097,#158098,#158099,#158100,
#158101,#158102,#158103,#158104,#158105,#158106,#158107,#158108,#158109,
#158110,#158111,#158112,#158113,#158114,#158115,#158116,#158117,#158118,
#158119,#158120,#158121,#158122,#158123,#158124,#158125,#158126,#158127,
#158128,#158129,#158130,#158131,#158132,#158133,#158134,#158135,#158136,
#158137,#158138,#158139,#158140,#158141,#158142,#158143,#158144,#158145,
#158146,#158147,#158148,#158149,#158150,#158151,#158152,#158153,#158154,
#158155,#158156,#158157,#158158,#158159,#158160,#158161,#158162,#158163,
#158164,#158165,#158166,#158167,#158168,#158169,#158170,#158171,#158172,
#158173,#158174,#158175,#158176,#158177,#158178,#158179,#158180,#158181,
#158182,#158183,#158184,#158185,#158186,#158187,#158188,#158189,#158190,
#158191,#158192,#158193,#158194,#158195,#158196,#158197,#158198,#158199,
#158200,#158201,#158202,#158203,#158204,#158205,#158206,#158207,#158208,
#158209,#158210,#158211,#158212,#158213,#158214,#158215,#158216,#158217,
#158218,#158219,#158220,#158221,#158222,#158223,#158224,#158225,#158226,
#158227,#158228,#158229,#158230,#158231,#158232,#158233,#158234,#158235,
#158236,#158237,#158238,#158239,#158240,#158241,#158242,#158243,#158244,
#158245,#158246,#158247,#158248,#158249,#158250,#158251,#158252,#158253,
#158254,#158255,#158256,#158257,#158258,#158259,#158260,#158261,#158262,
#158263,#158264,#158265,#158266,#158267,#158268,#158269,#158270,#158271,
#158272,#158273,#158274,#158275,#158276,#158277,#158278,#158279,#158280,
#158281,#158282,#158283,#158284,#158285,#158286,#158287,#158288,#158289,
#158290,#158291,#158292,#158293,#158294,#158295,#158296,#158297,#158298,
#158299,#158300,#158301,#158302,#158303,#158304,#158305,#158306,#158307,
#158308,#158309,#158310,#158311,#158312),.UNSPECIFIED.,.F.,.F.,(4,3,3,3,
3,3,3,3,3,3,3,3,3,3,3,3,3,3,3,3,3,3,3,3,3,3,3,3,3,3,3,3,3,3,3,3,3,3,3,3,
3,3,3,3,3,3,3,3,3,3,3,3,3,3,3,3,3,3,3,3,3,3,3,3,3,3,3,3,3,3,3,3,3,3,3,4),
(7.59153924858055,7.6845224783778,7.77753299194077,7.79755996417604,7.88864771831868,
7.97971760835622,8.07079089443809,8.16186028956199,8.2529495047339,8.28490746193705,
8.37600661966196,8.46708750385086,8.55817107950977,8.64925032934122,8.74034868496834,
8.77225495969805,8.86358446014535,8.95489727790249,9.04621272797726,9.13752315628156,
9.22884970421161,9.25960245745905,9.35004563389331,9.44046838421938,9.53089683726842,
9.62132426183796,9.71178086513476,9.74694995522005,9.83977082466953,9.93258020493847,
10.0253815422507,10.1181658427925,10.2109349487687,10.2342974529811,10.3226340982603,
10.4109484628818,10.4992807310775,10.5876214045936,10.6760195929041,10.7216449507421,
10.8172935625052,10.9152182840046,11.0107916985716,11.1098920735374,11.2089924485031,
11.2974475293379,11.3858999834853,11.4743988429813,11.5629222999095,11.6515265886469,
11.6963399462641,11.7845988436236,11.8727845281299,11.96091671564,12.0496814939083,
12.1377836965724,12.2258943659517,12.3140313137176,12.4032822207347,12.4915724815489,
12.5813037116675,12.6710349417861,12.7563666072233,12.8415825207838,12.9267064287632,
13.0117619568872,13.0967819333776,13.1817864079043,13.2667966276969,13.3518338433476,
13.4369714570383,13.5221663247904,13.6074971372277,13.6457299373081,13.7757706988632,
13.8747245557601),.UNSPECIFIED.);
#1700=B_SPLINE_CURVE_WITH_KNOTS('',3,(#158318,#158319,#158320,#158321,#158322,
#158323,#158324,#158325,#158326,#158327,#158328,#158329,#158330,#158331,
#158332),.UNSPECIFIED.,.F.,.F.,(4,1,1,1,1,1,1,1,1,1,1,1,4),(2.0217817672715,
2.43673748880501,2.92408498656602,3.41143248432702,3.89877998208802,4.38612747984903,
4.87347497761003,5.36082247537103,5.84816997313203,6.33551747089303,6.82286496865404,
7.31021246641504,7.59153924858053),.UNSPECIFIED.);
#1701=B_SPLINE_CURVE_WITH_KNOTS('',3,(#158335,#158336,#158337,#158338,#158339,
#158340,#158341,#158342,#158343,#158344,#158345,#158346,#158347,#158348,
#158349,#158350,#158351,#158352,#158353,#158354,#158355,#158356,#158357,
#158358,#158359,#158360,#158361,#158362,#158363,#158364,#158365,#158366,
#158367,#158368),.UNSPECIFIED.,.F.,.F.,(4,2,2,2,2,2,2,2,2,2,2,2,2,2,2,2,
4),(2.0822795579724E-5,0.091991742256264,0.179274456734732,0.298803049019205,
0.380584217944318,0.503956148693981,0.586127319892338,0.756537131127894,
0.827746482729973,0.952032398654662,1.0317636690925,1.111360273655,1.23017564205823,
1.31025989550073,1.44909386849414,1.58459957318183,1.64862342708563),
 .UNSPECIFIED.);
#1702=B_SPLINE_CURVE_WITH_KNOTS('',3,(#158373,#158374,#158375,#158376,#158377,
#158378,#158379,#158380,#158381,#158382,#158383,#158384,#158385,#158386,
#158387,#158388,#158389,#158390,#158391,#158392,#158393,#158394,#158395,
#158396,#158397,#158398,#158399,#158400,#158401,#158402,#158403,#158404,
#158405,#158406,#158407,#158408,#158409,#158410,#158411,#158412,#158413,
#158414,#158415,#158416,#158417,#158418,#158419,#158420,#158421,#158422,
#158423,#158424,#158425,#158426,#158427,#158428,#158429,#158430,#158431,
#158432,#158433,#158434,#158435,#158436,#158437,#158438,#158439,#158440,
#158441,#158442,#158443,#158444,#158445,#158446,#158447,#158448,#158449,
#158450,#158451,#158452,#158453,#158454,#158455,#158456,#158457,#158458,
#158459,#158460,#158461,#158462,#158463,#158464,#158465,#158466,#158467,
#158468,#158469,#158470,#158471,#158472,#158473,#158474,#158475,#158476,
#158477,#158478,#158479,#158480,#158481,#158482,#158483,#158484,#158485,
#158486,#158487,#158488,#158489,#158490,#158491,#158492,#158493,#158494,
#158495,#158496,#158497,#158498,#158499,#158500,#158501,#158502,#158503,
#158504,#158505,#158506,#158507,#158508,#158509,#158510,#158511,#158512,
#158513,#158514,#158515,#158516,#158517,#158518,#158519,#158520,#158521,
#158522,#158523,#158524,#158525,#158526,#158527,#158528,#158529,#158530,
#158531,#158532,#158533,#158534,#158535,#158536,#158537,#158538,#158539,
#158540,#158541,#158542,#158543,#158544,#158545,#158546,#158547,#158548,
#158549,#158550,#158551,#158552,#158553,#158554,#158555,#158556,#158557,
#158558,#158559,#158560,#158561,#158562,#158563,#158564,#158565,#158566,
#158567,#158568,#158569,#158570,#158571,#158572,#158573,#158574,#158575,
#158576,#158577,#158578,#158579,#158580,#158581,#158582,#158583,#158584,
#158585,#158586,#158587,#158588,#158589,#158590,#158591,#158592,#158593,
#158594,#158595,#158596,#158597,#158598),.UNSPECIFIED.,.F.,.F.,(4,3,3,3,
3,3,3,3,3,3,3,3,3,3,3,3,3,3,3,3,3,3,3,3,3,3,3,3,3,3,3,3,3,3,3,3,3,3,3,3,
3,3,3,3,3,3,3,3,3,3,3,3,3,3,3,3,3,3,3,3,3,3,3,3,3,3,3,3,3,3,3,3,3,3,3,4),
(7.59153924858053,7.68452254538593,7.77753312315871,7.79755996417604,7.88864761488148,
7.97971740157217,8.07079058546456,8.16185987934358,8.25294899549126,8.28490746193705,
8.37600652726715,8.46708731777341,8.55817079881157,8.6492499537383,8.74034821484695,
8.77225495969805,8.86358513560277,8.9548986330717,9.04621476194116,9.1375258664909,
9.22885308111593,9.25960245745905,9.35004385837792,9.44046482582385,9.53089150074111,
9.62131715354628,9.7117720080883,9.74694995522006,9.83977478998513,9.93258815792015,
10.025393459506,10.1181816912061,10.2109546401573,10.2342974529811,10.3226295283866,
10.410939313145,10.4992670123095,10.5876031247876,10.6759967918602,10.7216449507421,
10.8173001765085,10.9152232445072,11.0108032234786,11.1098978359908,11.2089924485031,
11.2974448715171,11.3858946564481,11.4743908456245,11.562911632656,11.6515132694445,
11.6963399462641,11.7845989400825,11.872784715549,11.9609169884106,12.0496817325825,
12.1377840060822,12.22589474066,12.31403174787,12.403282546349,12.4915728517076,
12.5813038967469,12.6710349417861,12.7563671078331,12.8415835245525,12.9267079378408,
13.011763973049,13.0967844578901,13.1817894416759,13.2668001713248,13.3518378971159,
13.4369760189292,13.5221713946028,13.6075027101629,13.6457299373081,13.775760012771,
13.8747245557601),.UNSPECIFIED.);
#1703=B_SPLINE_CURVE_WITH_KNOTS('',3,(#158599,#158600,#158601,#158602,#158603,
#158604,#158605,#158606,#158607,#158608,#158609,#158610,#158611,#158612,
#158613,#158614,#158615,#158616,#158617,#158618,#158619,#158620,#158621,
#158622,#158623,#158624,#158625,#158626,#158627,#158628,#158629,#158630,
#158631,#158632,#158633,#158634,#158635,#158636,#158637,#158638,#158639,
#158640,#158641,#158642,#158643,#158644,#158645,#158646,#158647,#158648,
#158649,#158650,#158651,#158652,#158653,#158654),.UNSPECIFIED.,.F.,.F.,
(4,2,2,2,2,2,2,2,2,2,2,2,2,2,2,2,2,2,2,2,2,2,2,2,2,2,2,4),(1.64862342708563,
1.65975747808592,1.7902957319901,1.89082544682229,1.95810743753247,2.04083689546831,
2.16778132685088,2.3015693448455,2.38012496633507,2.5075505762483,2.58030073732943,
2.72350721335624,2.80814921045046,2.89213912604029,3.05885293405854,3.13849080231745,
3.22533403256793,3.30933341472838,3.47596438146038,3.55560238516295,3.63426033790054,
3.7566778859009,3.82826608880163,3.99872817063951,4.08070038166504,4.19269628700354,
4.26378911976537,4.33594015439032),.UNSPECIFIED.);
#1704=B_SPLINE_CURVE_WITH_KNOTS('',3,(#158659,#158660,#158661,#158662,#158663,
#158664,#158665,#158666,#158667,#158668,#158669,#158670,#158671,#158672,
#158673,#158674,#158675,#158676,#158677,#158678,#158679,#158680,#158681,
#158682,#158683,#158684,#158685,#158686,#158687,#158688,#158689,#158690,
#158691,#158692,#158693,#158694,#158695,#158696,#158697,#158698,#158699,
#158700,#158701,#158702,#158703,#158704,#158705,#158706,#158707,#158708,
#158709,#158710,#158711,#158712,#158713,#158714,#158715,#158716,#158717,
#158718,#158719,#158720,#158721,#158722,#158723,#158724),.UNSPECIFIED.,
 .F.,.F.,(4,2,2,2,2,2,2,2,2,2,2,2,2,2,2,2,2,2,2,2,2,2,2,2,2,2,2,2,2,2,2,
2,4),(2.63429014437239,2.66088071416629,2.74224077834121,2.82343586597364,
2.94015381581752,3.00738688395098,3.13228218594895,3.20336250272686,3.37372653651136,
3.45586556153257,3.57847340338257,3.65999611372759,3.77619619405356,3.85543902504589,
3.97445736545625,4.06450248924364,4.17267568339614,4.24357042392699,4.40856429324298,
4.49003136565494,4.5999968004622,4.66211636333309,4.76327748018164,4.897186414341,
4.97452871563384,4.99842278741062,5.02879770385687,5.11926810911955,5.16652795741294,
5.19356119390082,5.22090478708735,5.26966811136063,5.32075006326628),
 .UNSPECIFIED.);
#1705=B_SPLINE_CURVE_WITH_KNOTS('',3,(#158725,#158726,#158727,#158728,#158729,
#158730,#158731,#158732,#158733,#158734,#158735,#158736,#158737,#158738,
#158739,#158740,#158741,#158742,#158743,#158744,#158745,#158746,#158747,
#158748,#158749,#158750,#158751,#158752,#158753,#158754,#158755,#158756,
#158757,#158758,#158759,#158760,#158761,#158762,#158763,#158764,#158765,
#158766,#158767,#158768,#158769,#158770,#158771,#158772,#158773,#158774,
#158775,#158776,#158777,#158778,#158779,#158780,#158781,#158782,#158783,
#158784,#158785,#158786,#158787,#158788,#158789,#158790,#158791,#158792,
#158793,#158794,#158795,#158796,#158797,#158798,#158799,#158800,#158801,
#158802,#158803,#158804,#158805,#158806,#158807,#158808,#158809,#158810,
#158811,#158812,#158813,#158814,#158815,#158816,#158817,#158818,#158819,
#158820,#158821,#158822,#158823,#158824,#158825,#158826,#158827,#158828,
#158829,#158830,#158831,#158832,#158833,#158834,#158835,#158836,#158837,
#158838,#158839,#158840,#158841,#158842,#158843,#158844,#158845,#158846,
#158847,#158848,#158849,#158850,#158851,#158852,#158853,#158854,#158855,
#158856,#158857,#158858,#158859,#158860,#158861,#158862,#158863,#158864,
#158865,#158866,#158867,#158868,#158869,#158870,#158871,#158872,#158873,
#158874,#158875,#158876,#158877,#158878,#158879,#158880,#158881,#158882,
#158883,#158884,#158885,#158886,#158887,#158888,#158889,#158890,#158891,
#158892,#158893,#158894,#158895,#158896,#158897,#158898,#158899,#158900,
#158901,#158902,#158903,#158904,#158905,#158906,#158907,#158908,#158909,
#158910,#158911,#158912,#158913,#158914,#158915,#158916,#158917,#158918,
#158919,#158920,#158921,#158922,#158923,#158924,#158925,#158926,#158927,
#158928,#158929,#158930,#158931,#158932,#158933,#158934,#158935,#158936,
#158937,#158938,#158939,#158940,#158941,#158942,#158943,#158944),
 .UNSPECIFIED.,.F.,.F.,(4,3,3,3,3,3,3,3,3,3,3,3,3,3,3,3,3,3,3,3,3,3,3,3,
3,3,3,3,3,3,3,3,3,3,3,3,3,3,3,3,3,3,3,3,3,3,3,3,3,3,3,3,3,3,3,3,3,3,3,3,
3,3,3,3,3,3,3,3,3,3,3,3,3,4),(-16.4213910178811,-16.3286400772641,-16.2359063591921,
-16.1431843748859,-16.0824674261131,-15.9941362568266,-15.9058273801709,
-15.8175005869686,-15.7291653788733,-15.6407726083022,-15.5951199283521,
-15.4994633914501,-15.4015406512354,-15.3059593709262,-15.2068659007586,
-15.1077724305911,-15.0193205338912,-14.9308712775328,-14.84237561715,-14.7538553588308,
-14.6652542472042,-14.6204249328301,-14.5321659202474,-14.4439801271102,
-14.3558478376921,-14.2670831001441,-14.1789808129682,-14.0908700658319,
-14.0027330472036,-13.9134822697297,-13.8251919559008,-13.7354609466044,
-13.6457299373081,-13.5603976716426,-13.4751811547976,-13.390056640956,
-13.3050005048409,-13.2199799188415,-13.1349748337167,-13.0499640026098,
-12.9649261753039,-12.8797879523774,-12.7945924756304,-12.7092610599517,
-12.6710349417861,-12.5825724970548,-12.4942229702032,-12.4059664919653,
-12.3172631737526,-12.2291341894402,-12.1410334445326,-12.0529431219476,
-11.9637923280267,-11.8756386254687,-11.7859892858664,-11.6963399462641,
-11.6077363315675,-11.5191997074042,-11.430713147944,-11.3422570464542,
-11.253802873335,-11.2089924485031,-11.1135865925285,-11.0156011820819,
-10.9199878797786,-10.8208164152604,-10.7216449507421,-10.633251005582,
-10.5449059290958,-10.4565828165548,-10.3682740267808,-10.2799419404527,
-10.2342974529811,-10.1382057107015),.UNSPECIFIED.);
#1706=B_SPLINE_CURVE_WITH_KNOTS('',3,(#158951,#158952,#158953,#158954,#158955,
#158956,#158957,#158958,#158959,#158960,#158961,#158962,#158963,#158964,
#158965,#158966,#158967,#158968,#158969,#158970,#158971,#158972,#158973,
#158974,#158975,#158976,#158977,#158978,#158979,#158980,#158981,#158982,
#158983,#158984,#158985,#158986,#158987,#158988,#158989,#158990,#158991,
#158992,#158993,#158994,#158995,#158996,#158997,#158998,#158999,#159000,
#159001,#159002),.UNSPECIFIED.,.F.,.F.,(4,2,2,2,2,2,2,2,2,2,2,2,2,2,2,2,
2,2,2,2,2,2,2,2,2,4),(2.08238338275598E-5,0.148644181152497,0.210319588588462,
0.2776422993658,0.445271649608167,0.529235565856092,0.612053706044955,0.726635154445241,
0.806859868487811,0.92542411935065,1.00702343966239,1.12918939140297,1.21136341657824,
1.38178387358329,1.45314145090535,1.57771255755794,1.65588566918239,1.73550298209199,
1.9026055656601,1.98658157752837,2.07050619976682,2.21332409776297,2.28618452567342,
2.41365385153232,2.49217608938517,2.63429014437239),.UNSPECIFIED.);
#1707=B_SPLINE_CURVE_WITH_KNOTS('',3,(#159003,#159004,#159005,#159006,#159007,
#159008,#159009,#159010,#159011,#159012,#159013,#159014,#159015,#159016,
#159017,#159018,#159019,#159020,#159021,#159022,#159023,#159024,#159025,
#159026,#159027,#159028,#159029,#159030,#159031,#159032,#159033,#159034,
#159035,#159036,#159037,#159038,#159039,#159040,#159041,#159042,#159043,
#159044,#159045,#159046,#159047,#159048,#159049,#159050,#159051,#159052,
#159053,#159054,#159055,#159056),.UNSPECIFIED.,.F.,.F.,(4,2,2,2,2,2,2,2,
2,2,2,2,2,2,2,2,2,2,2,2,2,2,2,2,2,2,4),(-2.68789745416103,-2.65408891563111,
-2.57621233738422,-2.49662198266966,-2.32905050023497,-2.24509032345514,
-2.17225591620052,-2.0550889100482,-1.97374945158346,-1.85231675710463,
-1.68441600725825,-1.51608472119004,-1.44252169241835,-1.30207874924859,
-1.21379570613023,-1.12981739078958,-0.980009160723121,-0.912778914788848,
-0.811762682087948,-0.682239388614031,-0.609249910766953,-0.468421195864385,
-0.38529873131632,-0.301417960888188,-0.150653053921509,-0.0760139026597096,
-0.000831891555311156),.UNSPECIFIED.);
#1708=B_SPLINE_CURVE_WITH_KNOTS('',3,(#159062,#159063,#159064,#159065,#159066,
#159067,#159068,#159069,#159070,#159071),.UNSPECIFIED.,.F.,.F.,(4,3,3,4),
(7.59252172359162,7.7065020665742,7.82442144880896,7.94234083104372),
 .UNSPECIFIED.);
#1709=B_SPLINE_CURVE_WITH_KNOTS('',3,(#159073,#159074,#159075,#159076,#159077,
#159078,#159079,#159080,#159081,#159082,#159083,#159084,#159085,#159086,
#159087,#159088,#159089,#159090,#159091,#159092,#159093,#159094,#159095,
#159096,#159097,#159098,#159099,#159100,#159101,#159102,#159103,#159104,
#159105,#159106,#159107,#159108,#159109,#159110,#159111,#159112,#159113,
#159114,#159115,#159116,#159117,#159118,#159119,#159120,#159121,#159122,
#159123,#159124,#159125,#159126,#159127,#159128,#159129,#159130,#159131,
#159132,#159133,#159134,#159135,#159136,#159137,#159138,#159139,#159140,
#159141,#159142,#159143,#159144,#159145,#159146,#159147,#159148,#159149,
#159150,#159151,#159152,#159153,#159154,#159155,#159156,#159157,#159158,
#159159,#159160,#159161,#159162,#159163,#159164,#159165,#159166,#159167,
#159168,#159169,#159170,#159171,#159172,#159173,#159174,#159175,#159176,
#159177,#159178,#159179,#159180,#159181,#159182,#159183,#159184,#159185,
#159186,#159187,#159188,#159189,#159190,#159191,#159192,#159193,#159194,
#159195,#159196,#159197,#159198,#159199,#159200,#159201,#159202,#159203,
#159204,#159205,#159206,#159207,#159208,#159209,#159210,#159211,#159212,
#159213,#159214,#159215,#159216,#159217,#159218,#159219,#159220,#159221,
#159222,#159223,#159224,#159225,#159226,#159227,#159228,#159229,#159230,
#159231,#159232,#159233,#159234,#159235,#159236,#159237,#159238,#159239,
#159240,#159241),.UNSPECIFIED.,.F.,.F.,(4,3,3,3,3,3,3,3,3,3,3,3,3,3,3,3,
3,3,3,3,3,3,3,3,3,3,3,3,3,3,3,3,3,3,3,3,3,3,3,3,3,3,3,3,3,3,3,3,3,3,3,3,
3,3,3,3,4),(2.00878451684803,2.11210413325299,2.21527034106239,2.31831513543185,
2.42129472868236,2.5242432661129,2.62719484999983,2.73025123525852,2.8333646167449,
2.93665426095938,2.99650934988562,3.1000823486418,3.20350565405811,3.30681236784354,
3.41005649077507,3.5132717780959,3.61649194455095,3.7198211439703,3.82320814715697,
3.92677824242682,3.9953457998475,4.09860802522564,4.2017148865668,4.30469822083937,
4.40761486436262,4.51049905109399,4.61338497056927,4.71637738346397,4.81942565840243,
4.92265765147002,4.99418224980938,5.09760362616701,5.20087164810082,5.30401837089651,
5.40709969299362,5.51014961192928,5.61320208205137,5.71636116106689,5.81957642889854,
5.92297408622033,5.99301869977125,6.09643424801845,6.19969680809051,6.30283864671347,
6.4059154433207,6.50896120312501,6.61200988851895,6.71516579043373,6.81837821646041,
6.92177360855697,6.99185514973313,7.09670696673363,7.20139077180048,7.30591382970463,
7.41034205932222,7.51471157544563,7.59252172323623),.UNSPECIFIED.);
#1710=B_SPLINE_CURVE_WITH_KNOTS('',3,(#159245,#159246,#159247,#159248,#159249,
#159250,#159251,#159252,#159253,#159254,#159255,#159256,#159257,#159258,
#159259,#159260,#159261,#159262,#159263,#159264,#159265,#159266,#159267,
#159268,#159269,#159270,#159271,#159272,#159273,#159274,#159275,#159276,
#159277,#159278,#159279,#159280,#159281,#159282,#159283,#159284,#159285,
#159286,#159287,#159288,#159289,#159290,#159291,#159292,#159293,#159294,
#159295,#159296,#159297,#159298,#159299,#159300,#159301,#159302,#159303,
#159304,#159305,#159306,#159307,#159308,#159309,#159310,#159311,#159312,
#159313,#159314,#159315,#159316,#159317,#159318,#159319,#159320,#159321,
#159322,#159323,#159324,#159325,#159326,#159327,#159328,#159329,#159330,
#159331,#159332,#159333,#159334,#159335,#159336,#159337,#159338,#159339,
#159340,#159341,#159342,#159343,#159344,#159345,#159346,#159347,#159348,
#159349,#159350,#159351,#159352,#159353,#159354,#159355,#159356,#159357,
#159358,#159359,#159360,#159361,#159362),.UNSPECIFIED.,.F.,.F.,(4,3,3,3,
3,3,3,3,3,3,3,3,3,3,3,3,3,3,3,3,3,3,3,3,3,3,3,3,3,3,3,3,3,3,3,3,3,3,3,4),
(-3.84103903298818,-3.73547282260036,-3.63371534234889,-3.53202565145685,
-3.4303680185594,-3.32870676083673,-3.22694496855287,-3.12512265123955,
-3.0231391421579,-2.99650934988562,-2.89298815672398,-2.78961796441274,
-2.68636610744672,-2.58317789200701,-2.48001949625454,-2.37685713986037,
-2.27358681231212,-2.17025936584276,-2.0667493147523,-1.99767289992375,
-1.8953694703404,-1.79322009387015,-1.69118812153633,-1.58921885584019,
-1.48727693124249,-1.38532702267508,-1.28325476444039,-1.1811195089167,
-1.07877855598727,-0.998836449961877,-0.892562814926303,-0.780992463060515,
-0.675072152100643,-0.569251436963408,-0.463502577326272,-0.357797922575414,
-0.252080134297595,-0.146357262849723,-0.0405614307760777,0.),
 .UNSPECIFIED.);
#1711=B_SPLINE_CURVE_WITH_KNOTS('',3,(#159363,#159364,#159365,#159366,#159367,
#159368,#159369,#159370,#159371,#159372,#159373,#159374,#159375,#159376,
#159377,#159378,#159379,#159380,#159381,#159382,#159383,#159384,#159385,
#159386,#159387,#159388),.UNSPECIFIED.,.F.,.F.,(4,2,2,2,2,2,2,2,2,2,2,2,
4),(0.000655563710817076,0.0215326330434009,0.0285520766491148,0.0303960653396223,
0.0316335621891305,0.0326484304910992,0.0337175099689998,0.035063400016696,
0.0377854527867724,0.0559548979009775,0.0616383509433211,0.073938246871362,
0.074757351053836),.UNSPECIFIED.);
#1712=B_SPLINE_CURVE_WITH_KNOTS('',3,(#159394,#159395,#159396,#159397,#159398,
#159399,#159400,#159401,#159402,#159403,#159404,#159405,#159406,#159407,
#159408,#159409,#159410,#159411,#159412,#159413,#159414,#159415,#159416,
#159417),.UNSPECIFIED.,.F.,.F.,(4,2,2,2,2,2,2,2,2,2,2,4),(2.59380941840705,
2.61949833194367,2.62782998250212,2.64083525297948,2.64309079252698,2.64448016828688,
2.64555519787246,2.6465640106262,2.6477771754924,2.64956358113838,2.65529879757913,
2.6679672673912),.UNSPECIFIED.);
#1713=B_SPLINE_CURVE_WITH_KNOTS('',3,(#159418,#159419,#159420,#159421,#159422,
#159423,#159424,#159425,#159426,#159427,#159428,#159429,#159430,#159431,
#159432,#159433,#159434,#159435,#159436,#159437,#159438,#159439,#159440,
#159441,#159442,#159443,#159444,#159445,#159446,#159447,#159448,#159449,
#159450,#159451,#159452,#159453,#159454,#159455,#159456,#159457,#159458,
#159459,#159460,#159461,#159462,#159463,#159464,#159465,#159466,#159467,
#159468,#159469,#159470,#159471,#159472,#159473,#159474,#159475,#159476,
#159477,#159478,#159479,#159480,#159481,#159482,#159483,#159484,#159485,
#159486,#159487,#159488,#159489,#159490,#159491,#159492,#159493,#159494,
#159495,#159496,#159497,#159498,#159499,#159500,#159501,#159502,#159503,
#159504,#159505,#159506,#159507,#159508,#159509,#159510,#159511,#159512,
#159513,#159514,#159515,#159516,#159517,#159518,#159519,#159520,#159521,
#159522,#159523,#159524,#159525,#159526,#159527,#159528,#159529,#159530,
#159531,#159532,#159533,#159534,#159535,#159536,#159537,#159538,#159539,
#159540,#159541,#159542,#159543,#159544,#159545,#159546,#159547,#159548,
#159549,#159550,#159551,#159552,#159553,#159554,#159555,#159556,#159557,
#159558,#159559,#159560,#159561,#159562,#159563,#159564,#159565,#159566,
#159567,#159568,#159569,#159570,#159571,#159572,#159573,#159574,#159575,
#159576,#159577,#159578,#159579,#159580,#159581,#159582,#159583,#159584,
#159585,#159586,#159587,#159588,#159589,#159590,#159591,#159592,#159593,
#159594,#159595,#159596,#159597,#159598),.UNSPECIFIED.,.F.,.F.,(4,3,3,3,
3,3,3,3,3,3,3,3,3,3,3,3,3,3,3,3,3,3,3,3,3,3,3,3,3,3,3,3,3,3,3,3,3,3,3,3,
3,3,3,3,3,3,3,3,3,3,3,3,3,3,3,3,3,3,3,3,4),(7.94234083104372,7.99069159969501,
8.0940913275558,8.19733763713527,8.30046266003865,8.40352230159087,8.50655059164692,
8.60958151690829,8.7127193321595,8.81591346077179,8.91929041688598,8.98952804965688,
9.09292506229385,9.19616867712089,9.29929104945922,9.40234806908498,9.5053737698128,
9.60840214233485,9.71153747947761,9.81472916791518,9.91810377272564,9.98836449961875,
10.0917566139964,10.1949952315025,10.2981124825157,10.4011643071107,10.5041847466055,
10.6072077991242,10.7103377621749,10.8135240379095,10.9168932275747,10.9872009495806,
11.0905965473409,11.1938386983577,11.2969595406341,11.4000149901819,11.5030390830394,
11.6060658120829,11.7091994619474,11.8123894359749,11.9157623013739,11.9860373995425,
12.0894323595201,12.1926738712652,12.2957940752146,12.3988488873555,12.5018723446726,
12.6048984409897,12.7080314669147,12.811220820953,12.9145930796965,12.9848738495044,
13.0869196145448,13.1887917815621,13.2905669727719,13.3922809390561,13.4939693462706,
13.5957283236005,13.6975219982505,13.7994743367661,13.8757070301447),
 .UNSPECIFIED.);
#1714=B_SPLINE_CURVE_WITH_KNOTS('',3,(#159599,#159600,#159601,#159602,#159603,
#159604,#159605,#159606,#159607,#159608,#159609,#159610,#159611,#159612,
#159613,#159614,#159615,#159616,#159617,#159618,#159619,#159620,#159621,
#159622,#159623,#159624,#159625,#159626,#159627,#159628,#159629,#159630,
#159631,#159632,#159633,#159634,#159635,#159636,#159637,#159638,#159639,
#159640,#159641,#159642,#159643,#159644,#159645,#159646,#159647,#159648,
#159649,#159650,#159651,#159652,#159653,#159654,#159655,#159656,#159657,
#159658,#159659,#159660,#159661,#159662,#159663,#159664,#159665,#159666,
#159667,#159668,#159669,#159670,#159671,#159672,#159673,#159674,#159675,
#159676,#159677,#159678,#159679,#159680,#159681,#159682,#159683,#159684,
#159685,#159686,#159687,#159688,#159689,#159690,#159691,#159692,#159693,
#159694,#159695,#159696,#159697,#159698,#159699,#159700,#159701,#159702,
#159703,#159704,#159705,#159706,#159707,#159708,#159709,#159710,#159711,
#159712,#159713,#159714,#159715,#159716,#159717,#159718,#159719,#159720,
#159721,#159722,#159723,#159724,#159725,#159726,#159727,#159728,#159729,
#159730,#159731,#159732,#159733,#159734,#159735,#159736,#159737,#159738,
#159739,#159740,#159741,#159742,#159743,#159744,#159745,#159746,#159747,
#159748,#159749,#159750,#159751,#159752,#159753,#159754,#159755,#159756,
#159757,#159758,#159759,#159760,#159761,#159762,#159763,#159764,#159765,
#159766,#159767,#159768,#159769,#159770,#159771,#159772,#159773,#159774,
#159775,#159776,#159777,#159778,#159779,#159780,#159781,#159782,#159783,
#159784,#159785,#159786,#159787,#159788,#159789,#159790,#159791,#159792,
#159793,#159794,#159795,#159796,#159797,#159798,#159799,#159800,#159801,
#159802,#159803,#159804,#159805,#159806,#159807,#159808,#159809,#159810,
#159811,#159812,#159813,#159814,#159815,#159816,#159817,#159818,#159819,
#159820,#159821,#159822,#159823,#159824),.UNSPECIFIED.,.F.,.F.,(4,2,2,2,
2,2,2,2,2,2,2,2,2,2,2,2,2,2,2,2,2,2,2,2,2,2,2,2,2,2,2,2,2,2,2,2,2,2,2,2,
2,2,2,2,2,2,2,2,2,2,2,2,2,2,2,2,2,2,2,2,2,2,2,2,2,2,2,2,2,2,2,2,2,2,2,2,
2,2,2,2,2,2,2,2,2,2,2,2,2,2,2,2,2,2,2,2,2,2,2,2,2,2,2,2,2,2,2,2,2,2,2,2,
4),(0.074757351053836,0.0845186006271381,0.106384720369821,0.122977204701593,
0.133286118471798,0.136520268752298,0.13858070105593,0.140506700555815,
0.14302476099034,0.147271566494101,0.192337918981624,0.220918010067583,
0.234451219159256,0.241869149971209,0.24384153295974,0.244851249473479,
0.245918287764432,0.247244906105232,0.249294243898364,0.258883319395038,
0.3185052212326,0.335297135910069,0.345718964687879,0.348985015376971,0.351065311525898,
0.353009687999067,0.355551683841704,0.359839378056905,0.394232083271677,
0.443433526167964,0.453286919760675,0.455474619338454,0.456715624008577,
0.457791888078883,0.45917051636006,0.462028237367567,0.484798677090485,
0.527329496551497,0.545904454581738,0.557102081967094,0.560449586097021,
0.56254524789876,0.564478990190647,0.56697181951992,0.571099362687016,0.598278838588343,
0.640350242366268,0.656908819361003,0.665449689147922,0.667534971515463,
0.668750089568529,0.669826541244136,0.671211292004528,0.673503748486762,
0.687289037325189,0.698622663609266,0.737950132216815,0.76449239524729,
0.7706604151559,0.773322046300717,0.775273867550828,0.777074383184398,0.779989388965879,
0.787184927175935,0.833861216483231,0.856214070304714,0.870037768760637,
0.875062851503067,0.878645349335746,0.880154639072828,0.88124607318625,
0.882271358494309,0.884011337224492,0.888723725450285,0.929075723453271,
0.977359055648121,0.982966790681687,0.985530047890678,0.987467724308793,
0.989297591964075,0.99185020792562,0.99855740676454,1.05366048101905,1.07817666552133,
1.0891211768874,1.09137327690968,1.09262569462842,1.09369779571862,1.09505198513576,
1.09779132550046,1.11614970864161,1.16514966527817,1.18898300462541,1.19480672617711,
1.19740893234859,1.19935222315296,1.20117008089484,1.20367844172205,1.21011171035855,
1.26784056735071,1.290703056673,1.30119586194948,1.30341928478801,1.30466495396065,
1.30573723518031,1.3070991638523,1.30978754870971,1.32763512700414,1.33373204601547,
1.37574265174544,1.40292854550757,1.40705404758681,1.40817977855291),
 .UNSPECIFIED.);
#1715=B_SPLINE_CURVE_WITH_KNOTS('',3,(#159829,#159830,#159831,#159832,#159833,
#159834,#159835,#159836,#159837,#159838,#159839,#159840,#159841,#159842,
#159843,#159844,#159845,#159846,#159847,#159848,#159849,#159850,#159851,
#159852,#159853,#159854,#159855,#159856,#159857,#159858,#159859,#159860,
#159861,#159862,#159863,#159864,#159865,#159866,#159867,#159868,#159869,
#159870,#159871,#159872,#159873,#159874,#159875,#159876,#159877,#159878,
#159879,#159880,#159881,#159882,#159883,#159884,#159885,#159886,#159887,
#159888,#159889,#159890,#159891,#159892,#159893,#159894,#159895,#159896,
#159897,#159898,#159899,#159900,#159901,#159902,#159903,#159904,#159905,
#159906,#159907,#159908,#159909,#159910,#159911,#159912,#159913,#159914,
#159915,#159916,#159917,#159918,#159919,#159920,#159921,#159922,#159923,
#159924,#159925,#159926,#159927,#159928,#159929,#159930,#159931,#159932,
#159933,#159934,#159935,#159936,#159937,#159938,#159939,#159940,#159941,
#159942,#159943,#159944,#159945,#159946,#159947,#159948,#159949,#159950,
#159951,#159952,#159953,#159954,#159955,#159956,#159957,#159958,#159959,
#159960,#159961,#159962,#159963,#159964,#159965,#159966,#159967,#159968,
#159969,#159970,#159971,#159972,#159973,#159974,#159975,#159976,#159977,
#159978,#159979,#159980,#159981,#159982,#159983,#159984,#159985,#159986,
#159987,#159988,#159989,#159990,#159991,#159992,#159993,#159994,#159995,
#159996,#159997,#159998,#159999,#160000,#160001,#160002,#160003,#160004,
#160005,#160006,#160007,#160008,#160009,#160010,#160011,#160012,#160013,
#160014,#160015,#160016,#160017,#160018,#160019,#160020,#160021,#160022,
#160023,#160024,#160025,#160026,#160027,#160028,#160029,#160030,#160031,
#160032,#160033,#160034,#160035,#160036,#160037,#160038,#160039,#160040,
#160041,#160042,#160043,#160044,#160045,#160046,#160047,#160048,#160049,
#160050,#160051,#160052,#160053,#160054,#160055,#160056,#160057,#160058,
#160059,#160060,#160061,#160062,#160063,#160064,#160065,#160066,#160067,
#160068),.UNSPECIFIED.,.F.,.F.,(4,2,2,2,2,2,2,2,2,2,2,2,2,2,2,2,2,2,2,2,
2,2,2,2,2,2,2,2,2,2,2,2,2,2,2,2,2,2,2,2,2,2,2,2,2,2,2,2,2,2,2,2,2,2,2,2,
2,2,2,2,2,2,2,2,2,2,2,2,2,2,2,2,2,2,2,2,2,2,2,2,2,2,2,2,2,2,2,2,2,2,2,2,
2,2,2,2,2,2,2,2,2,2,2,2,2,2,2,2,2,2,2,2,2,2,2,2,2,2,2,4),(1.2600599106657,
1.26288912535391,1.26546672182187,1.26740659099323,1.2692321791735,1.27176863481297,
1.2783722939111,1.33461433894213,1.35356859569969,1.36857213176709,1.37092236730132,
1.37232497219055,1.37340466478055,1.37461133465257,1.37665672191293,1.38470193621912,
1.39984346049816,1.43954686638813,1.4708057047285,1.4750324770183,1.47755426186251,
1.47949234347171,1.48157483792521,1.48486313000707,1.49551763572174,1.51284659152949,
1.55313561931878,1.58013059772863,1.58303313425721,1.58441975480281,1.58549471901526,
1.58672467901592,1.58887517585962,1.59827196371131,1.64751324121126,1.68273421234887,
1.68703164173585,1.6895739237452,1.69151526139603,1.69358910344686,1.69683824331718,
1.70714740115669,1.7237054019932,1.75659509515038,1.77015013463504,1.77746533608878,
1.78181876712263,1.79298904519116,1.7951431604594,1.79650197108491,1.79757435442588,
1.79882307623579,1.80105931569587,1.81175029489963,1.83532213563743,1.8919015926996,
1.89846487221822,1.90099476188535,1.90281852965995,1.90475915087935,1.90734233483733,
1.91305921724745,1.93608540191422,1.9691538244237,1.99055890719327,2.00472993237957,
2.00704303828902,2.0084346488703,2.00951273409787,2.01072527727021,2.01279764212641,
2.02117128946334,2.03724274418735,2.07957429992307,2.10704942593072,2.11118323019587,
2.11367758936683,2.11561117618825,2.11770532539845,2.12104748652128,2.13219934534976,
2.15066840242999,2.1966441165456,2.21638857299317,2.21917013134654,2.22053281879586,
2.22160543750744,2.22285120126972,2.22507416361126,2.23555385409372,2.25836439253159,
2.31613632519638,2.32256110393637,2.32506828750695,2.32688602427336,2.32882987004577,
2.33143399807762,2.33726698227413,2.36116976346223,2.39067207230513,2.42835862256573,
2.43118386681462,2.43255516416355,2.43362846043887,2.43484317647371,2.43695337153951,
2.43956179473568,2.44500433206508,2.46056097646302,2.50211803345605,2.51357722963294,
2.53186992066977,2.53558058707372,2.5379739042411,2.53989032669438,2.54206276619736,
2.54575859597035,2.56078603352987,2.58950540908657,2.59380941840705),
 .UNSPECIFIED.);
#1716=B_SPLINE_CURVE_WITH_KNOTS('',3,(#160070,#160071,#160072,#160073,#160074,
#160075,#160076,#160077,#160078,#160079,#160080,#160081,#160082,#160083,
#160084,#160085,#160086,#160087,#160088,#160089,#160090,#160091,#160092,
#160093,#160094,#160095,#160096,#160097,#160098,#160099,#160100,#160101,
#160102,#160103,#160104,#160105,#160106,#160107,#160108,#160109,#160110,
#160111,#160112,#160113,#160114,#160115,#160116,#160117,#160118,#160119,
#160120,#160121,#160122,#160123,#160124,#160125,#160126,#160127,#160128,
#160129,#160130,#160131,#160132,#160133,#160134,#160135,#160136,#160137,
#160138,#160139,#160140,#160141,#160142,#160143,#160144,#160145,#160146,
#160147,#160148,#160149,#160150,#160151,#160152,#160153,#160154,#160155,
#160156,#160157,#160158,#160159,#160160,#160161,#160162,#160163,#160164,
#160165,#160166,#160167,#160168,#160169,#160170,#160171,#160172,#160173,
#160174,#160175,#160176,#160177,#160178,#160179,#160180,#160181,#160182,
#160183,#160184,#160185,#160186,#160187,#160188,#160189,#160190,#160191,
#160192,#160193,#160194,#160195,#160196,#160197,#160198,#160199,#160200,
#160201,#160202,#160203,#160204,#160205,#160206,#160207,#160208,#160209,
#160210,#160211,#160212,#160213,#160214,#160215,#160216,#160217,#160218,
#160219,#160220,#160221,#160222,#160223,#160224,#160225,#160226,#160227,
#160228,#160229,#160230,#160231,#160232,#160233,#160234,#160235,#160236,
#160237,#160238,#160239,#160240,#160241,#160242,#160243,#160244,#160245,
#160246,#160247,#160248,#160249,#160250,#160251,#160252,#160253,#160254,
#160255,#160256,#160257,#160258,#160259,#160260,#160261,#160262,#160263,
#160264,#160265,#160266,#160267,#160268,#160269,#160270,#160271,#160272,
#160273,#160274,#160275,#160276,#160277,#160278,#160279),.UNSPECIFIED.,
 .F.,.F.,(4,2,2,2,2,2,2,2,2,2,2,2,2,2,2,2,2,2,2,2,2,2,2,2,2,2,2,2,2,2,2,
2,2,2,2,2,2,2,2,2,2,2,2,2,2,2,2,2,2,2,2,2,2,2,2,2,2,2,2,2,2,2,2,2,2,2,2,
2,2,2,2,2,2,2,2,2,2,2,2,2,2,2,2,2,2,2,2,2,2,2,2,2,2,2,2,2,2,2,2,2,2,2,2,
2,4),(1.40817977855291,1.40954560774862,1.41147833506768,1.41357286092246,
1.41691845439741,1.4281081550461,1.44666702024889,1.49069794755451,1.49656825849803,
1.51244823923978,1.51506158494816,1.51640744724944,1.51747862028056,1.51873640342676,
1.52101503627392,1.53242870530449,1.55875529228532,1.61123422194255,1.61816336074522,
1.62103577801428,1.62282984191506,1.62479053342678,1.62749310835263,1.63388990777096,
1.68179592775418,1.72137458067039,1.72610766369619,1.72785087794966,1.72887686407961,
1.72996902851074,1.73147804058059,1.73505270627621,1.77423000471657,1.82298217096951,
1.83011257534725,1.83301838131916,1.83481850841655,1.83677410191252,1.83944843119071,
1.84568035406849,1.87272167021881,1.91344481746139,1.93614292237264,1.93899640814411,
1.94037316759951,1.94144684594556,1.94268250749392,1.9448600448532,1.95465124329529,
2.00353490506446,2.03864076811217,2.04293545333154,2.04547651168061,2.04741714484553,
2.04949045706281,2.05273923143588,2.06305113699394,2.07961724078901,2.11250757355492,
2.12707356620539,2.13238380146595,2.14842375962974,2.15104510417974,2.15239272485768,
2.15346399684019,2.15472036241686,2.15699278370449,2.16830033571824,2.19420980535604,
2.24727808148534,2.25416218722088,2.25702698438639,2.25881950642072,2.26078109800886,
2.26348965088267,2.26992299273335,2.29863021547031,2.34984370580904,2.360880822129,
2.36302633640549,2.36438233186787,2.3654542289635,2.36670437704547,2.36894815971249,
2.37977009097098,2.40382815546894,2.45963793744676,2.46627614938373,2.46881749744398,
2.47064395100252,2.47252001071295,2.47500421270246,2.47774234321234,2.48229405495379,
2.49162484745556,2.54226102660567,2.57203624611155,2.57495061686113,2.57633922955457,
2.57741405239469,2.57864196533992,2.58078446075229,2.59007763691164,2.60891631395619,
2.66742168200086),.UNSPECIFIED.);
#1717=B_SPLINE_CURVE_WITH_KNOTS('',3,(#160280,#160281,#160282,#160283),
 .UNSPECIFIED.,.F.,.F.,(4,4),(-16.7565929213048,-16.4074096477818),
 .UNSPECIFIED.);
#1718=B_SPLINE_CURVE_WITH_KNOTS('',3,(#160289,#160290,#160291,#160292,#160293,
#160294,#160295,#160296,#160297,#160298,#160299,#160300,#160301,#160302,
#160303,#160304),.UNSPECIFIED.,.F.,.F.,(4,2,2,2,2,2,2,4),(2.60093440570636,
2.65621612731345,2.66440519623879,2.66748629392595,2.66932347326792,2.67117334794446,
2.67347254279515,2.67554350108758),.UNSPECIFIED.);
#1719=B_SPLINE_CURVE_WITH_KNOTS('',3,(#160305,#160306,#160307,#160308,#160309,
#160310,#160311,#160312,#160313,#160314,#160315,#160316,#160317,#160318,
#160319,#160320,#160321,#160322,#160323,#160324,#160325,#160326,#160327,
#160328,#160329,#160330,#160331,#160332,#160333,#160334,#160335,#160336,
#160337,#160338,#160339,#160340,#160341,#160342,#160343,#160344,#160345,
#160346,#160347,#160348,#160349,#160350,#160351,#160352,#160353,#160354,
#160355,#160356,#160357,#160358,#160359,#160360,#160361,#160362,#160363,
#160364,#160365,#160366,#160367,#160368,#160369,#160370,#160371,#160372,
#160373,#160374,#160375,#160376,#160377,#160378,#160379,#160380,#160381,
#160382,#160383,#160384,#160385,#160386,#160387,#160388,#160389,#160390,
#160391,#160392,#160393,#160394,#160395,#160396,#160397,#160398,#160399,
#160400,#160401,#160402,#160403,#160404,#160405,#160406,#160407,#160408,
#160409,#160410,#160411,#160412,#160413,#160414,#160415,#160416,#160417,
#160418,#160419,#160420,#160421,#160422,#160423,#160424,#160425,#160426,
#160427,#160428,#160429,#160430,#160431,#160432,#160433,#160434,#160435,
#160436,#160437,#160438,#160439,#160440,#160441,#160442,#160443,#160444,
#160445,#160446,#160447,#160448,#160449,#160450,#160451,#160452,#160453,
#160454,#160455,#160456,#160457,#160458,#160459,#160460,#160461,#160462,
#160463,#160464,#160465,#160466,#160467,#160468,#160469,#160470,#160471,
#160472,#160473,#160474,#160475,#160476,#160477,#160478,#160479,#160480,
#160481,#160482,#160483,#160484,#160485,#160486,#160487,#160488,#160489,
#160490,#160491,#160492,#160493,#160494,#160495,#160496,#160497,#160498,
#160499,#160500,#160501,#160502,#160503,#160504,#160505,#160506,#160507,
#160508,#160509,#160510,#160511,#160512,#160513,#160514,#160515,#160516,
#160517,#160518,#160519,#160520,#160521,#160522,#160523,#160524,#160525,
#160526,#160527,#160528,#160529,#160530,#160531,#160532,#160533,#160534,
#160535,#160536,#160537,#160538,#160539,#160540,#160541,#160542,#160543,
#160544,#160545,#160546,#160547,#160548,#160549,#160550,#160551,#160552,
#160553,#160554,#160555,#160556),.UNSPECIFIED.,.F.,.F.,(4,2,2,2,2,2,2,2,
2,2,2,2,2,2,2,2,2,2,2,2,2,2,2,2,2,2,2,2,2,2,2,2,2,2,2,2,2,2,2,2,2,2,2,2,
2,2,2,2,2,2,2,2,2,2,2,2,2,2,2,2,2,2,2,2,2,2,2,2,2,2,2,2,2,2,2,2,2,2,2,2,
2,2,2,2,2,2,2,2,2,2,2,2,2,2,2,2,2,2,2,2,2,2,2,2,2,2,2,2,2,2,2,2,2,2,2,2,
2,2,2,2,2,2,2,2,2,4),(0.000823831819623115,0.00401800839811174,0.0104924304194195,
0.0605869953018769,0.0859355292913153,0.0970980150654373,0.0993620175889886,
0.10061653242929,0.101687951053084,0.1030379450659,0.105670338168074,0.121948896835917,
0.172208828757248,0.190225336365632,0.20118167184012,0.203640691931348,
0.205924449585136,0.205939156587538,0.205954465836589,0.205970417579372,
0.205987055811404,0.206004428922813,0.206022590221724,0.20604159843857,
0.206061518650619,0.206082423055476,0.206104392100308,0.206127515721166,
0.20615189484137,0.206177643148387,0.206204889295696,0.20623377954482,0.206264481016142,
0.206297185733427,0.206332115692975,0.208204369316481,0.210580155753786,
0.214996727511496,0.240374125406916,0.284126697672046,0.300798382684377,
0.309377389810547,0.31146587329223,0.312681813631161,0.313758847935915,
0.315143836398988,0.317435001369859,0.331166304045355,0.332819697931548,
0.33712537014045,0.353432760491326,0.386321840025734,0.402920312468902,
0.413247881169353,0.416498451223915,0.418572163273139,0.420512647622365,
0.42305275830711,0.427344188489171,0.462475421859073,0.511405738160027,
0.521174752265968,0.523350854337974,0.524586228623091,0.52565999932951,
0.527037317024668,0.529893490512413,0.566048497467635,0.598719807973166,
0.621173215863973,0.626812880026451,0.629381690192194,0.631319865414483,
0.633147475528139,0.63569254512669,0.642353070409631,0.698011138240209,
0.722204159617916,0.733062373940504,0.735308617144993,0.736559414429266,
0.737631420146538,0.738986973908385,0.741733085117442,0.760301425460177,
0.77499048799126,0.777696345221885,0.810492717848545,0.833138515677649,
0.838804483371501,0.841378282182323,0.843317379454756,0.845143771971418,
0.847683797876563,0.854311170321881,0.910310110498169,0.934284976020168,
0.945084794477429,0.94732765831116,0.948577795322991,0.949649988534673,
0.9510067460488,0.953154191892558,0.964217252849379,1.01536489706998,1.04409104779892,
1.05052796189061,1.05323756827982,1.05519976166513,1.05699272657523,1.05985798688195,
1.06674190988961,1.11989087671858,1.14579192987643,1.15709805182436,1.15937088844298,
1.16062756331162,1.16169916403531,1.16304726993864,1.16566973867728,1.18171851092261,
1.18583066515089,1.20152335318015,1.23441379642287,1.25720344504392,1.2600599106657),
 .UNSPECIFIED.);
#1720=B_SPLINE_CURVE_WITH_KNOTS('',3,(#160558,#160559,#160560,#160561,#160562,
#160563,#160564,#160565,#160566,#160567),.UNSPECIFIED.,.F.,.F.,(4,1,1,1,
1,1,1,4),(-22.6905949549614,-21.9744018991612,-20.9755654491994,-19.9767289992375,
-18.9778925492756,-17.9790560993137,-16.9802196493519,-16.7565929213048),
 .UNSPECIFIED.);
#1721=B_SPLINE_CURVE_WITH_KNOTS('',3,(#160568,#160569,#160570,#160571,#160572,
#160573,#160574,#160575,#160576,#160577,#160578,#160579,#160580,#160581,
#160582,#160583,#160584,#160585),.UNSPECIFIED.,.F.,.F.,(4,2,2,2,2,2,2,2,
4),(0.000629331620540443,0.0475078168467217,0.0567255773861956,0.0588625698839201,
0.060089245776326,0.0611642454588925,0.0625547407310968,0.06481439862756,
0.0747558145485526),.UNSPECIFIED.);
#1722=B_SPLINE_CURVE_WITH_KNOTS('',3,(#160590,#160591,#160592,#160593,#160594,
#160595,#160596,#160597,#160598,#160599,#160600,#160601,#160602,#160603,
#160604,#160605,#160606,#160607,#160608,#160609,#160610,#160611,#160612,
#160613,#160614,#160615,#160616,#160617,#160618,#160619,#160620,#160621,
#160622,#160623,#160624,#160625,#160626,#160627,#160628,#160629,#160630,
#160631,#160632,#160633,#160634,#160635,#160636,#160637,#160638,#160639,
#160640,#160641,#160642,#160643,#160644,#160645,#160646,#160647,#160648,
#160649,#160650,#160651,#160652,#160653,#160654,#160655,#160656,#160657,
#160658,#160659,#160660,#160661,#160662,#160663,#160664,#160665,#160666,
#160667,#160668,#160669,#160670,#160671,#160672,#160673,#160674,#160675,
#160676,#160677,#160678,#160679,#160680,#160681,#160682,#160683,#160684,
#160685,#160686,#160687,#160688,#160689,#160690,#160691,#160692,#160693,
#160694,#160695,#160696,#160697,#160698,#160699,#160700,#160701,#160702,
#160703,#160704,#160705,#160706,#160707,#160708,#160709,#160710,#160711,
#160712,#160713,#160714,#160715,#160716,#160717,#160718,#160719,#160720,
#160721,#160722,#160723,#160724,#160725,#160726,#160727,#160728,#160729,
#160730,#160731,#160732,#160733,#160734,#160735,#160736,#160737,#160738,
#160739,#160740,#160741,#160742,#160743,#160744,#160745,#160746,#160747,
#160748,#160749,#160750,#160751,#160752,#160753,#160754,#160755,#160756,
#160757,#160758,#160759,#160760,#160761,#160762,#160763,#160764,#160765,
#160766,#160767,#160768,#160769,#160770,#160771,#160772,#160773,#160774,
#160775,#160776,#160777,#160778,#160779,#160780,#160781,#160782,#160783,
#160784,#160785,#160786,#160787,#160788,#160789,#160790,#160791,#160792,
#160793,#160794,#160795,#160796,#160797,#160798,#160799,#160800,#160801,
#160802,#160803,#160804,#160805,#160806,#160807,#160808,#160809,#160810,
#160811,#160812,#160813,#160814,#160815,#160816,#160817,#160818,#160819,
#160820,#160821,#160822,#160823,#160824,#160825,#160826,#160827,#160828,
#160829,#160830,#160831),.UNSPECIFIED.,.F.,.F.,(4,2,2,2,2,2,2,2,2,2,2,2,
2,2,2,2,2,2,2,2,2,2,2,2,2,2,2,2,2,2,2,2,2,2,2,2,2,2,2,2,2,2,2,2,2,2,2,2,
2,2,2,2,2,2,2,2,2,2,2,2,2,2,2,2,2,2,2,2,2,2,2,2,2,2,2,2,2,2,2,2,2,2,2,2,
2,2,2,2,2,2,2,2,2,2,2,2,2,2,2,2,2,2,2,2,2,2,2,2,2,2,2,2,2,2,2,2,2,2,2,2,
4),(1.26320710672139,1.28140414234432,1.28500138353877,1.28651711084254,
1.28761306789754,1.28864171356143,1.29038764403513,1.29511760263283,1.33565551298413,
1.33755091949281,1.38151516558556,1.38876004482394,1.39169055907568,1.39349930084687,
1.39545899299493,1.39812949461983,1.40430979044002,1.43085974961406,1.46989942006753,
1.47806737419444,1.49539616576754,1.49807318164083,1.49943531608537,1.50051080902851,
1.50176370969853,1.50400882264022,1.51476846237791,1.53854565703878,1.56600522890494,
1.59803832250086,1.60229132438091,1.60482450173032,1.60676886200393,1.60885567636036,
1.61214565537418,1.62276072883805,1.63998156816887,1.68585974467617,1.69266243201266,
1.70814828222705,1.71052335679931,1.71193530537155,1.71301888120648,1.71422622885667,
1.71626478862146,1.72418361242935,1.73895518628867,1.76807925458489,1.81059592893948,
1.81490262956325,1.81745143083311,1.81939834275103,1.82147871760401,1.82473929995121,
1.8350949481432,1.85173731670276,1.8847536489348,1.90082106962562,1.90452585779774,
1.920728118739,1.92336197728496,1.92471486669975,1.92578970689773,1.92704953480292,
1.92932642430623,1.9406196402055,1.9664132761091,2.01994414452875,2.02682825603955,
2.02969870608222,2.03149640617639,2.0334649855724,2.03618561413902,2.04265916874073,
2.07162167809736,2.12175094590221,2.13377890667838,2.13598737190434,2.13736477749226,
2.13844157309132,2.13968378436968,2.14187999043465,2.15187508517746,2.20077284354723,
2.23592774949268,2.24024341448053,2.24279474285378,2.24474198657402,2.24682116726395,
2.25007664697864,2.26038889830554,2.27693571456329,2.30987152969426,2.31640056354918,
2.34567293588195,2.34859595355489,2.34998889435175,2.35106716279007,2.35229911889678,
2.35444892062684,2.36377767365169,2.38269482948208,2.39296685265398,2.44514301688019,
2.45212081150089,2.45500959828721,2.45681058500777,2.45873684234103,2.46136102539072,
2.46429298621507,2.4854012479541,2.54037683814402,2.55864646498026,2.56135594357227,
2.56272500282369,2.5638010622619,2.56504902496354,2.56727149592393,2.57766883742916,
2.6001440379358,2.60093440570636),.UNSPECIFIED.);
#1723=B_SPLINE_CURVE_WITH_KNOTS('',3,(#160832,#160833,#160834,#160835,#160836,
#160837,#160838,#160839,#160840,#160841,#160842,#160843,#160844,#160845,
#160846,#160847,#160848,#160849,#160850,#160851,#160852,#160853,#160854,
#160855,#160856,#160857,#160858,#160859,#160860,#160861,#160862,#160863,
#160864,#160865,#160866,#160867,#160868,#160869,#160870,#160871,#160872,
#160873,#160874,#160875,#160876,#160877,#160878,#160879,#160880,#160881,
#160882,#160883,#160884,#160885,#160886,#160887,#160888,#160889,#160890,
#160891,#160892,#160893,#160894,#160895,#160896,#160897,#160898,#160899,
#160900,#160901,#160902,#160903,#160904,#160905,#160906,#160907,#160908,
#160909,#160910,#160911,#160912,#160913,#160914,#160915,#160916,#160917,
#160918,#160919,#160920,#160921,#160922,#160923,#160924,#160925,#160926,
#160927,#160928,#160929,#160930,#160931,#160932,#160933,#160934,#160935,
#160936,#160937,#160938,#160939,#160940,#160941,#160942,#160943,#160944,
#160945,#160946,#160947,#160948,#160949,#160950,#160951,#160952,#160953,
#160954,#160955,#160956,#160957,#160958,#160959,#160960,#160961,#160962,
#160963,#160964,#160965,#160966,#160967,#160968,#160969,#160970,#160971,
#160972,#160973,#160974,#160975,#160976,#160977,#160978,#160979,#160980,
#160981,#160982,#160983,#160984,#160985,#160986,#160987,#160988,#160989,
#160990,#160991,#160992,#160993,#160994,#160995,#160996,#160997,#160998,
#160999,#161000,#161001,#161002,#161003,#161004,#161005,#161006,#161007,
#161008,#161009,#161010,#161011,#161012,#161013,#161014,#161015,#161016,
#161017,#161018,#161019,#161020,#161021,#161022,#161023,#161024,#161025,
#161026,#161027,#161028,#161029,#161030,#161031,#161032,#161033,#161034,
#161035,#161036,#161037,#161038,#161039,#161040,#161041,#161042,#161043,
#161044,#161045,#161046,#161047,#161048,#161049,#161050,#161051,#161052,
#161053,#161054,#161055,#161056,#161057),.UNSPECIFIED.,.F.,.F.,(4,2,2,2,
2,2,2,2,2,2,2,2,2,2,2,2,2,2,2,2,2,2,2,2,2,2,2,2,2,2,2,2,2,2,2,2,2,2,2,2,
2,2,2,2,2,2,2,2,2,2,2,2,2,2,2,2,2,2,2,2,2,2,2,2,2,2,2,2,2,2,2,2,2,2,2,2,
2,2,2,2,2,2,2,2,2,2,2,2,2,2,2,2,2,2,2,2,2,2,2,2,2,2,2,2,2,2,2,2,2,2,2,2,
4),(0.0747558145485526,0.0779070904825867,0.120249644631008,0.145989993525991,
0.159965461628393,0.163505020842006,0.165684550070463,0.167599659799729,
0.169981431001474,0.173655430061543,0.191378664380046,0.19828890932858,
0.24295086429607,0.260025988150294,0.268741768545356,0.270841011506001,
0.272059362216972,0.273135947487221,0.274517035470703,0.276794899791266,
0.290252290912955,0.292360162179196,0.299136038197401,0.344049382673289,
0.361735742077373,0.372547926332288,0.375852888847452,0.377938563445688,
0.379874516979267,0.382386317486921,0.38658052038385,0.416415903625031,
0.457671852824752,0.472771237092085,0.480799656046433,0.482843161564643,
0.484049150480445,0.485128537416682,0.486531128281553,0.48888214920247,
0.503919283598053,0.511373094173349,0.524871568033967,0.557728188154391,
0.57428627654557,0.584595735868982,0.58784433778009,0.58991769076366,0.591858468787986,
0.594399872264172,0.598695522196392,0.633840746724231,0.682831924910063,
0.692532698189676,0.694704196495929,0.695938599229324,0.69701257859874,
0.698391542028116,0.701255880442206,0.737184343239716,0.791377344542833,
0.797845270892868,0.800559854167596,0.802522732508193,0.804314319922441,
0.807173032372063,0.814018747570061,0.8676263920037,0.893200794242408,0.90442244267948,
0.906690155055799,0.907945601780378,0.909017131748506,0.910366393328177,
0.912994780488261,0.929123567550305,0.929621525660078,0.973962052568461,
1.00333240209617,1.00984521440323,1.01256740304457,1.01453174461314,1.01632190637789,
1.01917237674873,1.02596775389844,1.08017868508287,1.10534321348777,1.11645879487501,
1.11872039385959,1.11997454835422,1.12104625245535,1.12239736356506,1.12503417777243,
1.14146547420592,1.19205473798027,1.20976653569563,1.22059034191823,1.22389689679959,
1.22598312505857,1.22791928177783,1.23043090597563,1.23462384918071,1.26436858768193,
1.30531332236539,1.32779341565066,1.33045688873952,1.33179575230525,1.33276374710846,
1.33398738364706,1.33610994526848,1.34512883071186,1.36311432695761,1.4083236437572),
 .UNSPECIFIED.);
#1724=B_SPLINE_CURVE_WITH_KNOTS('',3,(#161063,#161064,#161065,#161066,#161067,
#161068),.UNSPECIFIED.,.F.,.F.,(4,2,4),(2.59382545345877,2.60858976740298,
2.66828105520032),.UNSPECIFIED.);
#1725=B_SPLINE_CURVE_WITH_KNOTS('',3,(#161069,#161070,#161071,#161072,#161073,
#161074,#161075,#161076,#161077,#161078,#161079,#161080,#161081,#161082,
#161083,#161084,#161085,#161086,#161087,#161088,#161089,#161090,#161091,
#161092,#161093,#161094,#161095,#161096,#161097,#161098,#161099,#161100,
#161101,#161102,#161103,#161104,#161105,#161106,#161107,#161108,#161109,
#161110,#161111,#161112,#161113,#161114,#161115,#161116,#161117,#161118,
#161119,#161120,#161121,#161122,#161123,#161124,#161125,#161126,#161127,
#161128,#161129,#161130,#161131,#161132,#161133,#161134,#161135,#161136,
#161137,#161138,#161139,#161140,#161141,#161142,#161143,#161144,#161145,
#161146,#161147,#161148,#161149,#161150,#161151,#161152,#161153,#161154,
#161155,#161156,#161157,#161158,#161159,#161160,#161161,#161162,#161163,
#161164,#161165,#161166,#161167,#161168,#161169,#161170,#161171,#161172,
#161173,#161174,#161175,#161176,#161177,#161178,#161179,#161180,#161181,
#161182,#161183,#161184,#161185,#161186,#161187,#161188,#161189,#161190,
#161191,#161192,#161193,#161194,#161195,#161196,#161197,#161198,#161199,
#161200,#161201,#161202,#161203,#161204,#161205,#161206,#161207,#161208,
#161209,#161210,#161211,#161212,#161213,#161214,#161215,#161216,#161217,
#161218,#161219,#161220,#161221,#161222,#161223,#161224,#161225,#161226,
#161227,#161228,#161229,#161230,#161231,#161232,#161233,#161234,#161235,
#161236,#161237,#161238,#161239,#161240,#161241,#161242,#161243,#161244,
#161245,#161246,#161247,#161248,#161249,#161250,#161251,#161252,#161253,
#161254,#161255,#161256,#161257,#161258,#161259,#161260,#161261,#161262,
#161263,#161264,#161265,#161266,#161267,#161268,#161269,#161270,#161271,
#161272,#161273,#161274,#161275,#161276,#161277,#161278,#161279,#161280,
#161281,#161282,#161283,#161284,#161285,#161286,#161287,#161288,#161289,
#161290,#161291,#161292,#161293,#161294,#161295,#161296,#161297,#161298,
#161299,#161300),.UNSPECIFIED.,.F.,.F.,(4,2,2,2,2,2,2,2,2,2,2,2,2,2,2,2,
2,2,2,2,2,2,2,2,2,2,2,2,2,2,2,2,2,2,2,2,2,2,2,2,2,2,2,2,2,2,2,2,2,2,2,2,
2,2,2,2,2,2,2,2,2,2,2,2,2,2,2,2,2,2,2,2,2,2,2,2,2,2,2,2,2,2,2,2,2,2,2,2,
2,2,2,2,2,2,2,2,2,2,2,2,2,2,2,2,2,2,2,2,2,2,2,2,2,2,2,4),(0.000810718701221239,
0.00554260920676304,0.00881069049620377,0.0102445705775083,0.0113189793639876,
0.0123417958007916,0.013364997589063,0.0148060135692522,0.018652612309518,
0.0263910026761921,0.0833917197290533,0.101376797239213,0.112318970037956,
0.115637673150875,0.117726086427897,0.119660511337923,0.122164583149168,
0.126333317872102,0.155180738303453,0.200461313494667,0.213470785694448,
0.21829327494598,0.220684984061829,0.222655718012321,0.223833871222962,
0.223837515898326,0.223841183790664,0.223844881997329,0.224893785280639,
0.226286911041078,0.22859848991649,0.2426512180014,0.246702722448747,0.295875971010819,
0.320268890090069,0.326173935108442,0.328795347896809,0.330746248224604,
0.332566375929547,0.335070246102484,0.341451014444341,0.399907259755484,
0.422483015974022,0.432907130575143,0.435130958039406,0.436379033592028,
0.437454788729539,0.438822933631868,0.441001419341293,0.452511668185328,
0.456228031163227,0.458210453133546,0.507969235807919,0.532835636036655,
0.53880221340975,0.541434703689076,0.543387524753794,0.54520491588675,0.547697940995197,
0.554013729704037,0.612970783520306,0.644629005737836,0.647423945944726,
0.648791613782613,0.64985760339708,0.651102362889227,0.653253199647321,
0.661646900927268,0.66851258319867,0.676919549212547,0.690113838868585,
0.723067667516947,0.745876052435108,0.751571588847899,0.754155296717372,
0.756100431149762,0.757931462534918,0.760476262317749,0.767106219692119,
0.823431411539454,0.847370014597311,0.858172580304495,0.860420245030225,
0.861673653540622,0.862749020387333,0.864110265999117,0.866783348118166,
0.88400989640664,0.929650504394038,0.957595998133478,0.963947949737999,
0.966647900175744,0.968612685372211,0.970414651743481,0.973308820189539,
0.980337182079209,1.03183631782581,1.0590913619819,1.0707506369482,1.07304823960531,
1.07431253075116,1.07538696131069,1.07673398002563,1.07934075859183,1.09490105320128,
1.10149592559763,1.14300544954136,1.17035691015266,1.1766366096842,1.17932425579853,
1.18128691731234,1.18309169238097,1.18600087326701,1.19311889565946,1.24290532459789,
1.26320710672139),.UNSPECIFIED.);
#1726=B_SPLINE_CURVE_WITH_KNOTS('',3,(#161302,#161303,#161304,#161305,#161306,
#161307,#161308,#161309,#161310,#161311,#161312,#161313,#161314,#161315,
#161316,#161317,#161318,#161319,#161320,#161321,#161322,#161323,#161324,
#161325,#161326,#161327,#161328,#161329,#161330,#161331,#161332,#161333,
#161334,#161335,#161336,#161337,#161338,#161339,#161340,#161341,#161342,
#161343,#161344,#161345,#161346,#161347,#161348,#161349,#161350,#161351,
#161352,#161353,#161354,#161355,#161356,#161357,#161358,#161359,#161360,
#161361,#161362,#161363,#161364,#161365,#161366,#161367,#161368,#161369,
#161370,#161371,#161372,#161373,#161374,#161375,#161376,#161377,#161378,
#161379,#161380,#161381,#161382,#161383,#161384,#161385,#161386,#161387,
#161388,#161389,#161390,#161391,#161392,#161393,#161394,#161395,#161396,
#161397,#161398,#161399,#161400,#161401,#161402,#161403,#161404,#161405,
#161406,#161407,#161408,#161409,#161410,#161411,#161412,#161413,#161414,
#161415,#161416,#161417,#161418,#161419,#161420,#161421,#161422,#161423,
#161424,#161425,#161426,#161427,#161428,#161429,#161430,#161431,#161432,
#161433,#161434,#161435,#161436,#161437,#161438,#161439,#161440,#161441,
#161442,#161443,#161444,#161445,#161446,#161447,#161448,#161449,#161450,
#161451,#161452,#161453,#161454,#161455,#161456,#161457,#161458,#161459,
#161460,#161461,#161462,#161463,#161464,#161465,#161466,#161467,#161468,
#161469,#161470,#161471,#161472,#161473,#161474,#161475,#161476,#161477,
#161478,#161479,#161480,#161481,#161482,#161483,#161484,#161485,#161486,
#161487,#161488,#161489,#161490,#161491,#161492,#161493,#161494,#161495,
#161496,#161497,#161498,#161499,#161500,#161501,#161502,#161503,#161504,
#161505,#161506,#161507,#161508,#161509,#161510,#161511,#161512,#161513,
#161514,#161515,#161516,#161517,#161518,#161519,#161520,#161521,#161522,
#161523,#161524,#161525,#161526,#161527),.UNSPECIFIED.,.F.,.F.,(4,2,2,2,
2,2,2,2,2,2,2,2,2,2,2,2,2,2,2,2,2,2,2,2,2,2,2,2,2,2,2,2,2,2,2,2,2,2,2,2,
2,2,2,2,2,2,2,2,2,2,2,2,2,2,2,2,2,2,2,2,2,2,2,2,2,2,2,2,2,2,2,2,2,2,2,2,
2,2,2,2,2,2,2,2,2,2,2,2,2,2,2,2,2,2,2,2,2,2,2,2,2,2,2,2,2,2,2,2,2,2,2,2,
4),(1.4083236437572,1.41333088102273,1.43113507874003,1.43481460833219,
1.43719828185415,1.43911380859235,1.44129260787215,1.44501750954835,1.46042424063277,
1.51176001269828,1.53943960591465,1.54234661805959,1.54373395565199,1.54480881996912,
1.54603793152059,1.54818521995648,1.5575410729071,1.60680754718084,1.64203163357876,
1.64632838195724,1.6488702241749,1.65081120474635,1.65288464475482,1.65613311175937,
1.66643977270715,1.68299341831262,1.71587590631286,1.72932272850514,1.73690850471888,
1.75190581616602,1.75425534624431,1.75565756083092,1.75673697171553,1.75794334773225,
1.75998828226784,1.76803229050528,1.78317232121768,1.82287871736754,1.85411353439998,
1.85833888367202,1.86085992235106,1.86279749047767,1.86487949205803,1.86816713072526,
1.87882061679871,1.89614899638409,1.94436622567246,1.94866622868069,1.95164780867162,
1.964114487631,1.96634200506697,1.96772295144803,1.96879713313419,1.97003026604958,
1.97219594288744,1.98181269988829,2.03085053856742,2.06600585940044,2.07030157363753,
2.07284306510737,2.07478392816005,2.07685738836378,2.08010619126858,2.09041648203885,
2.1069783966275,2.13986700711218,2.15403049940507,2.1599766382467,2.17581378956652,
2.17842647832321,2.17977231448054,2.18084356398319,2.1821015189154,2.18438096846461,
2.19580920798741,2.22219368929917,2.27459135630503,2.28152570238893,2.28439890186766,
2.28619305096762,2.2881535114613,2.29085517423541,2.29724700768573,2.34319558300291,
2.36575831840106,2.37225027459431,2.38783353350176,2.39043517498929,2.39177859327856,
2.39284965042523,2.39410939384263,2.39639723893086,2.40797587152629,2.43496484031123,
2.47463666767185,2.49124595386254,2.49484613103896,2.49720516282961,2.49911867099566,
2.50092102866028,2.50411069483385,2.51448476108362,2.53127830882496,2.55157207583426,
2.59669168652602,2.60141377415054,2.60315522484572,2.6041807997957,2.60527312030848,
2.60678322172997,2.61036438665645,2.6481167165806,2.6673459870611),
 .UNSPECIFIED.);
#1727=B_SPLINE_CURVE_WITH_KNOTS('',3,(#161528,#161529,#161530,#161531,#161532,
#161533,#161534,#161535,#161536,#161537,#161538,#161539,#161540,#161541,
#161542,#161543,#161544,#161545,#161546,#161547),.UNSPECIFIED.,.F.,.F.,
(4,2,2,2,2,2,2,2,2,4),(0.000704181919289228,0.0257174334271328,0.0359847052706526,
0.0390634794182119,0.041189796444609,0.0432709609679292,0.045208316296964,
0.0477298861286788,0.0519579423206877,0.0751489568361618),.UNSPECIFIED.);
#1728=B_SPLINE_CURVE_WITH_KNOTS('',3,(#161552,#161553,#161554,#161555,#161556,
#161557,#161558,#161559,#161560,#161561,#161562,#161563,#161564,#161565,
#161566,#161567,#161568,#161569,#161570,#161571,#161572,#161573,#161574,
#161575,#161576,#161577,#161578,#161579,#161580,#161581,#161582,#161583,
#161584,#161585,#161586,#161587,#161588,#161589,#161590,#161591,#161592,
#161593,#161594,#161595,#161596,#161597,#161598,#161599,#161600,#161601,
#161602,#161603,#161604,#161605,#161606,#161607,#161608,#161609,#161610,
#161611,#161612,#161613,#161614,#161615,#161616,#161617,#161618,#161619,
#161620,#161621,#161622,#161623,#161624,#161625,#161626,#161627,#161628,
#161629,#161630,#161631,#161632,#161633,#161634,#161635,#161636,#161637,
#161638,#161639,#161640,#161641,#161642,#161643,#161644,#161645,#161646,
#161647,#161648,#161649,#161650,#161651,#161652,#161653,#161654,#161655,
#161656,#161657,#161658,#161659,#161660,#161661,#161662,#161663,#161664,
#161665,#161666,#161667,#161668,#161669,#161670,#161671,#161672,#161673,
#161674,#161675,#161676,#161677,#161678,#161679,#161680,#161681,#161682,
#161683,#161684,#161685,#161686,#161687,#161688,#161689,#161690,#161691,
#161692,#161693,#161694,#161695,#161696,#161697,#161698,#161699,#161700,
#161701,#161702,#161703,#161704,#161705,#161706,#161707,#161708,#161709,
#161710,#161711,#161712,#161713,#161714,#161715,#161716,#161717,#161718,
#161719,#161720,#161721,#161722,#161723,#161724,#161725,#161726,#161727,
#161728,#161729,#161730,#161731,#161732,#161733,#161734,#161735,#161736,
#161737,#161738,#161739,#161740,#161741,#161742,#161743,#161744,#161745,
#161746,#161747,#161748,#161749,#161750,#161751,#161752,#161753,#161754,
#161755,#161756,#161757,#161758,#161759,#161760,#161761,#161762,#161763,
#161764,#161765,#161766,#161767,#161768,#161769,#161770,#161771,#161772,
#161773,#161774,#161775,#161776,#161777,#161778,#161779,#161780,#161781,
#161782,#161783,#161784,#161785,#161786,#161787,#161788,#161789,#161790,
#161791,#161792,#161793,#161794,#161795,#161796,#161797,#161798,#161799,
#161800,#161801,#161802,#161803,#161804,#161805,#161806,#161807,#161808,
#161809,#161810,#161811,#161812,#161813,#161814,#161815,#161816,#161817,
#161818,#161819,#161820,#161821,#161822,#161823,#161824,#161825,#161826,
#161827,#161828,#161829,#161830,#161831,#161832,#161833,#161834,#161835),
 .UNSPECIFIED.,.F.,.F.,(4,2,2,2,2,2,2,2,2,2,2,2,2,2,2,2,2,2,2,2,2,2,2,2,
2,2,2,2,2,2,2,2,2,2,2,2,2,2,2,2,2,2,2,2,2,2,2,2,2,2,2,2,2,2,2,2,2,2,2,2,
2,2,2,2,2,2,2,2,2,2,2,2,2,2,2,2,2,2,2,2,2,2,2,2,2,2,2,2,2,2,2,2,2,2,2,2,
2,2,2,2,2,2,2,2,2,2,2,2,2,2,2,2,2,2,2,2,2,2,2,2,2,2,2,2,2,2,2,2,2,2,2,2,
2,2,2,2,2,2,2,2,2,4),(1.26013242656284,1.26847918134053,1.2938564122058,
1.29812711955091,1.30042465381827,1.30231772666777,1.3045584725669,1.30845763746593,
1.3243663415617,1.33458859927051,1.37387299698104,1.4024572161702,1.4053697735664,
1.40675832499297,1.40783346977875,1.40906216367256,1.41120699114716,1.42052526401983,
1.46970173840529,1.50507092651571,1.50937010626214,1.51191286829673,1.51385425276344,
1.51592783494069,1.51917592094151,1.52947628965138,1.54601499838239,1.57356179924573,
1.5897043460026,1.60078541295709,1.61502070589077,1.61733730448075,1.61872998294231,
1.61980826017967,1.62102030954763,1.6230902427204,1.6314329097389,1.64741501045388,
1.68972964697637,1.71734583451292,1.72148352025247,1.72397909849109,1.72591296472535,
1.72800675256841,1.73134689975681,1.7424786549331,1.76090055733768,1.80770061574921,
1.81249826086563,1.82339984547313,1.82845376648346,1.83024456505479,1.83128003435429,
1.83236713223855,1.83384477279152,1.83723798187632,1.84192243504985,1.85438809617534,
1.88539080905029,1.92909919171492,1.93338877780441,1.93592874243147,1.93786964938256,
1.93994433061575,1.94319750069632,1.95354238542488,1.97017964780189,2.00313452907881,
2.02128581528153,2.03881227559786,2.04149029520036,2.04285029656371,2.04392274505452,
2.04517053947875,2.04740263377742,2.05802725879118,2.08135818609268,2.13831025169886,
2.1448319530684,2.14735509137067,2.14917705166816,2.15111858720384,2.15370785936002,
2.1594584038067,2.18273718211609,2.2232585956789,2.2379885967061,2.25117560153088,
2.25344040570918,2.25483260280213,2.25590799356616,2.25713409396543,2.25926769005325,
2.26843475405723,2.31716148689409,2.35312562790782,2.35784809405546,2.36027128666429,
2.36219053876016,2.36434389000288,2.36795350025004,2.38192047521569,2.43273432932107,
2.46258728964277,2.4654995248621,2.46688790208378,2.46793103838049,2.46793599692886,
2.46794086746965,2.46794565197622,2.46795035244432,2.46795497071022,2.46795950855504,
2.46796396780665,2.46796835018156,2.46797265740426,2.46797689093535,2.46798105251445,
2.46798514361251,2.46798916574424,2.46799312034853,2.46799700881634,2.46800061011772,
2.46800419784891,2.46800777221051,2.46801133342244,2.4680148813335,2.46923820354584,
2.47054910125195,2.47257198390835,2.47638445811796,2.48565763471479,2.52352802125493,
2.53702592018721,2.56540108051988,2.56955862836313,2.57205996523756,2.57399461867134,
2.57608560313406,2.57941339266775,2.59043117045207,2.59382545345877),
 .UNSPECIFIED.);
#1729=B_SPLINE_CURVE_WITH_KNOTS('',3,(#161836,#161837,#161838,#161839,#161840,
#161841,#161842,#161843,#161844,#161845,#161846,#161847,#161848,#161849,
#161850,#161851,#161852,#161853,#161854,#161855,#161856,#161857,#161858,
#161859,#161860,#161861,#161862,#161863,#161864,#161865,#161866,#161867,
#161868,#161869,#161870,#161871,#161872,#161873,#161874,#161875,#161876,
#161877,#161878,#161879,#161880,#161881,#161882,#161883,#161884,#161885,
#161886,#161887,#161888,#161889,#161890,#161891,#161892,#161893,#161894,
#161895,#161896,#161897,#161898,#161899,#161900,#161901,#161902,#161903,
#161904,#161905,#161906,#161907,#161908,#161909,#161910,#161911,#161912,
#161913,#161914,#161915,#161916,#161917,#161918,#161919,#161920,#161921,
#161922,#161923,#161924,#161925,#161926,#161927,#161928,#161929,#161930,
#161931,#161932,#161933,#161934,#161935,#161936,#161937,#161938,#161939,
#161940,#161941,#161942,#161943,#161944,#161945,#161946,#161947,#161948,
#161949,#161950,#161951,#161952,#161953,#161954,#161955,#161956,#161957,
#161958,#161959,#161960,#161961,#161962,#161963,#161964,#161965,#161966,
#161967,#161968,#161969,#161970,#161971,#161972,#161973,#161974,#161975,
#161976,#161977,#161978,#161979,#161980,#161981,#161982,#161983,#161984,
#161985,#161986,#161987,#161988,#161989,#161990,#161991,#161992,#161993,
#161994,#161995,#161996,#161997,#161998,#161999,#162000,#162001,#162002,
#162003,#162004,#162005,#162006,#162007,#162008,#162009,#162010,#162011,
#162012,#162013,#162014,#162015,#162016,#162017,#162018,#162019,#162020,
#162021,#162022,#162023,#162024,#162025,#162026,#162027,#162028,#162029,
#162030,#162031,#162032,#162033,#162034,#162035,#162036,#162037,#162038,
#162039,#162040,#162041,#162042,#162043,#162044,#162045,#162046,#162047,
#162048,#162049,#162050,#162051,#162052,#162053,#162054,#162055,#162056,
#162057,#162058,#162059,#162060,#162061,#162062,#162063,#162064,#162065),
 .UNSPECIFIED.,.F.,.F.,(4,2,2,2,2,2,2,2,2,2,2,2,2,2,2,2,2,2,2,2,2,2,2,2,
2,2,2,2,2,2,2,2,2,2,2,2,2,2,2,2,2,2,2,2,2,2,2,2,2,2,2,2,2,2,2,2,2,2,2,2,
2,2,2,2,2,2,2,2,2,2,2,2,2,2,2,2,2,2,2,2,2,2,2,2,2,2,2,2,2,2,2,2,2,2,2,2,
2,2,2,2,2,2,2,2,2,2,2,2,2,2,2,2,2,2,4),(0.0751489568361618,0.0833449554465519,
0.108641044920857,0.13643639417136,0.145888780373659,0.148042561636215,
0.149272889427158,0.150347200439784,0.151731685845863,0.15397150696322,
0.166679492706045,0.189075522143858,0.21602105826756,0.237186514044569,
0.245292357039389,0.251237193407344,0.253852945759734,0.255807448099823,
0.257608548802691,0.260520314133154,0.267687292186551,0.315460101430164,
0.355564539204594,0.35916186777971,0.360674655778008,0.361767379036676,
0.362792108113141,0.364529513521338,0.369225456412141,0.4100672476177,0.456723676866092,
0.463116321672252,0.465818002434891,0.467778359893003,0.469572338490051,
0.472445086812289,0.4793774053219,0.531828880147045,0.558201172160656,0.569625398196958,
0.571904539571247,0.573162375005064,0.5742335568168,0.575579345175449,0.578192051861403,
0.594045473246712,0.598812469573507,0.614066862527545,0.646942646584495,
0.663524224601453,0.673844261091207,0.677094043431458,0.679167632965294,
0.681108269480274,0.683648964137022,0.68794224291894,0.730340769312746,
0.759394175981448,0.774119156147365,0.782012070532489,0.78404402550762,
0.785247464640317,0.786327541631833,0.78773492830596,0.790102318017432,
0.805539438786653,0.812257187230313,0.826054822290535,0.858915373230047,
0.875477569270088,0.885788964040406,0.889037844799358,0.891111296217081,
0.893052110514189,0.895593480881535,0.899888894180826,0.935008265132251,
0.98391811743147,0.993716904537488,0.995895161085198,0.997131070231455,
0.99820486564332,0.999581639982368,1.00243471029315,1.02510631592757,1.03806040668731,
1.07091616283321,1.08747013021954,1.0977781014675,1.10102680821244,1.10310036600066,
1.10504143261076,1.10758335377593,1.11188019211292,1.14707724642032,1.19622694753891,
1.20575167390782,1.20791111016212,1.20914295954032,1.21021749394502,1.2116008152167,
1.21383590954592,1.22644269909234,1.23297510085648,1.23810837803455,1.27817128215072,
1.30767505401814,1.31208547029223,1.31441240100971,1.31613949187338,1.31829592426455,
1.32191875657871,1.33436950633737,1.38533028477281,1.40863209392471),
 .UNSPECIFIED.);
#1730=B_SPLINE_CURVE_WITH_KNOTS('',3,(#162071,#162072,#162073,#162074,#162075,
#162076,#162077,#162078,#162079,#162080),.UNSPECIFIED.,.F.,.F.,(4,2,2,2,
4),(2.59333918514653,2.59405628316297,2.6039559079893,2.65275178216379,
2.66750871075831),.UNSPECIFIED.);
#1731=B_SPLINE_CURVE_WITH_KNOTS('',3,(#162081,#162082,#162083,#162084,#162085,
#162086,#162087,#162088,#162089,#162090,#162091,#162092,#162093,#162094,
#162095,#162096,#162097,#162098,#162099,#162100,#162101,#162102,#162103,
#162104,#162105,#162106,#162107,#162108,#162109,#162110,#162111,#162112,
#162113,#162114,#162115,#162116,#162117,#162118,#162119,#162120,#162121,
#162122,#162123,#162124,#162125,#162126,#162127,#162128,#162129,#162130,
#162131,#162132,#162133,#162134,#162135,#162136,#162137,#162138,#162139,
#162140,#162141,#162142,#162143,#162144,#162145,#162146,#162147,#162148,
#162149,#162150,#162151,#162152,#162153,#162154,#162155,#162156,#162157,
#162158,#162159,#162160,#162161,#162162,#162163,#162164,#162165,#162166,
#162167,#162168,#162169,#162170,#162171,#162172,#162173,#162174,#162175,
#162176,#162177,#162178,#162179,#162180,#162181,#162182,#162183,#162184,
#162185,#162186,#162187,#162188,#162189,#162190,#162191,#162192,#162193,
#162194,#162195,#162196,#162197,#162198,#162199,#162200,#162201,#162202,
#162203,#162204,#162205,#162206,#162207,#162208,#162209,#162210,#162211,
#162212,#162213,#162214,#162215,#162216,#162217,#162218,#162219,#162220,
#162221,#162222,#162223,#162224,#162225,#162226,#162227,#162228,#162229,
#162230,#162231,#162232,#162233,#162234,#162235,#162236,#162237,#162238,
#162239,#162240,#162241,#162242,#162243,#162244,#162245,#162246,#162247,
#162248,#162249,#162250,#162251,#162252,#162253,#162254,#162255,#162256,
#162257,#162258,#162259,#162260,#162261,#162262,#162263,#162264,#162265,
#162266,#162267,#162268,#162269,#162270,#162271,#162272,#162273,#162274,
#162275,#162276,#162277,#162278,#162279,#162280,#162281,#162282,#162283,
#162284,#162285,#162286,#162287,#162288,#162289,#162290,#162291,#162292,
#162293,#162294,#162295,#162296,#162297,#162298,#162299,#162300,#162301,
#162302,#162303,#162304),.UNSPECIFIED.,.F.,.F.,(4,2,2,2,2,2,2,2,2,2,2,2,
2,2,2,2,2,2,2,2,2,2,2,2,2,2,2,2,2,2,2,2,2,2,2,2,2,2,2,2,2,2,2,2,2,2,2,2,
2,2,2,2,2,2,2,2,2,2,2,2,2,2,2,2,2,2,2,2,2,2,2,2,2,2,2,2,2,2,2,2,2,2,2,2,
2,2,2,2,2,2,2,2,2,2,2,2,2,2,2,2,2,2,2,2,2,2,2,2,2,2,2,4),(0.000768646098525406,
0.0217309817958381,0.0248341135680857,0.0269704303777135,0.0287696752420724,
0.0306848669530417,0.0330688062049348,0.0367500644603691,0.0545889053194324,
0.072976426511539,0.121840731681455,0.131681559431032,0.133862402465048,
0.135098744280054,0.136172254774499,0.137547801196249,0.140395367973628,
0.176851300966736,0.209417973596582,0.225629647754282,0.232376498172673,
0.237517164998177,0.239979927065182,0.241821109356285,0.243648389985645,
0.24619263155957,0.252848770294063,0.308527217431946,0.332702250954838,
0.343555212971455,0.345800986701256,0.347051608827662,0.348123517583509,
0.349479016880949,0.351622788493995,0.362631176800057,0.41390476092387,
0.442559457110958,0.448987263154324,0.45169501212071,0.453656578007115,
0.455449463209985,0.458315670049848,0.465207432626328,0.518223304340964,
0.544204779337861,0.55553046951741,0.557804109580375,0.55906080818677,0.560132173748389,
0.561479658771376,0.564099964090362,0.580119165322993,0.585171725011565,
0.629884117999277,0.648404509572726,0.659579206323581,0.662923538439578,
0.66501800966143,0.666951188477761,0.669444035816599,0.673573230202735,
0.700872959537443,0.74313000808192,0.759409658662449,0.767854453894341,
0.76993243152354,0.771146140908599,0.772223829844904,0.773613062349352,
0.775918320327097,0.78993599693432,0.791300662880673,0.798313629024612,
0.811988486142423,0.844849500022869,0.861411040465311,0.871722287033649,
0.874971259424407,0.877044802557563,0.878985726048627,0.881527273081773,
0.885823060478109,0.920955452540655,0.969902002886644,0.979660845880634,
0.981836453631895,0.983071820463264,0.98414575958055,0.985523521937409,
0.988381404501232,1.01124164447141,1.02400683492131,1.05686258733372,1.07341533033534,
1.08372289663384,1.08697166607503,1.08904530962754,1.09098648866183,1.09352860343324,
1.09782587301926,1.13304060983893,1.18224601591773,1.19170998865719,1.19386521180401,
1.19509617320075,1.19617091431267,1.19755579201663,1.19979593007968,1.21249735659049,
1.23487541233553,1.26013242656284),.UNSPECIFIED.);
#1732=B_SPLINE_CURVE_WITH_KNOTS('',3,(#162306,#162307,#162308,#162309,#162310,
#162311,#162312,#162313,#162314,#162315,#162316,#162317,#162318,#162319,
#162320,#162321,#162322,#162323,#162324,#162325,#162326,#162327,#162328,
#162329,#162330,#162331,#162332,#162333,#162334,#162335,#162336,#162337,
#162338,#162339,#162340,#162341,#162342,#162343,#162344,#162345,#162346,
#162347,#162348,#162349,#162350,#162351,#162352,#162353,#162354,#162355,
#162356,#162357,#162358,#162359,#162360,#162361,#162362,#162363,#162364,
#162365,#162366,#162367,#162368,#162369,#162370,#162371,#162372,#162373,
#162374,#162375,#162376,#162377,#162378,#162379,#162380,#162381,#162382,
#162383,#162384,#162385,#162386,#162387,#162388,#162389,#162390,#162391,
#162392,#162393,#162394,#162395,#162396,#162397,#162398,#162399,#162400,
#162401,#162402,#162403,#162404,#162405,#162406,#162407,#162408,#162409,
#162410,#162411,#162412,#162413,#162414,#162415,#162416,#162417,#162418,
#162419,#162420,#162421,#162422,#162423,#162424,#162425,#162426,#162427,
#162428,#162429,#162430,#162431,#162432,#162433,#162434,#162435,#162436,
#162437,#162438,#162439,#162440,#162441,#162442,#162443,#162444,#162445,
#162446,#162447,#162448,#162449,#162450,#162451,#162452,#162453,#162454,
#162455,#162456,#162457,#162458,#162459,#162460,#162461,#162462,#162463,
#162464,#162465,#162466,#162467,#162468,#162469,#162470,#162471,#162472,
#162473,#162474,#162475,#162476,#162477,#162478,#162479,#162480,#162481,
#162482,#162483,#162484,#162485,#162486,#162487,#162488,#162489,#162490,
#162491,#162492,#162493,#162494,#162495,#162496,#162497,#162498,#162499,
#162500,#162501,#162502,#162503,#162504,#162505,#162506,#162507,#162508,
#162509,#162510,#162511,#162512,#162513,#162514,#162515,#162516,#162517,
#162518,#162519,#162520,#162521,#162522,#162523,#162524,#162525,#162526,
#162527,#162528,#162529,#162530,#162531),.UNSPECIFIED.,.F.,.F.,(4,2,2,2,
2,2,2,2,2,2,2,2,2,2,2,2,2,2,2,2,2,2,2,2,2,2,2,2,2,2,2,2,2,2,2,2,2,2,2,2,
2,2,2,2,2,2,2,2,2,2,2,2,2,2,2,2,2,2,2,2,2,2,2,2,2,2,2,2,2,2,2,2,2,2,2,2,
2,2,2,2,2,2,2,2,2,2,2,2,2,2,2,2,2,2,2,2,2,2,2,2,2,2,2,2,2,2,2,2,2,2,2,2,
4),(1.40863209392471,1.41654004015942,1.41945322232817,1.42084187779814,
1.42191701390898,1.42314559807403,1.42529000014722,1.43460280781364,1.48376179701782,
1.51915216916635,1.52345152062868,1.52599430522233,1.52793566143861,1.53000916937361,
1.5332570471261,1.54355598158733,1.56009165224911,1.5929619616422,1.60448792644199,
1.61424432011087,1.616083043487,1.62920572003994,1.63146738296949,1.63285867803094,
1.63393402438427,1.63516080211121,1.63729727256023,1.6465024232659,1.6650626351445,
1.70910389964158,1.73177230506072,1.73572450676605,1.73819157751035,1.74011589131014,
1.7422444183836,1.74574152273181,1.75844262846443,1.78069138277645,1.82661416362083,
1.84109882641281,1.84342683756833,1.84482287069084,1.84590159531708,1.84711174698918,
1.84917310970567,1.85741106613972,1.87309470335307,1.91500271990899,1.94340736467262,
1.94756591043407,1.9500676219038,1.95200243176961,1.95409345285052,1.95742101540776,
1.96843542360814,1.98658578893815,2.03627510442844,2.03766423139636,2.03787170234985,
2.04116319860353,2.05333850278761,2.05555053616329,2.05692693064984,2.05800083663026,
2.05923734118391,2.06141775571317,2.07124506207417,2.12011418295603,2.15521860878868,
2.15951431615174,2.16205602934499,2.16399719176571,2.16607109788608,2.1693208627816,
2.17963642647082,2.1962089237285,2.22910963071889,2.26471089204683,2.2675774835449,
2.26895701128334,2.27003118301784,2.27126553685399,2.27343629182438,2.28312333534856,
2.3321089936017,2.36725061824319,2.37154667908901,2.37408844848276,2.37602956573768,
2.37810333819365,2.38135271529671,2.39166554439082,2.40823221768773,2.47087662185185,
2.47223807011973,2.4784121202474,2.4803506188615,2.48153349538097,2.4825652255805,
2.48397838287725,2.48699359698213,2.4910919890305,2.50137087532382,2.52419460816738,
2.57590998757691,2.58289424438075,2.58577628814764,2.58757249419691,2.58953243240337,
2.59222832476124,2.59858285211227,2.62662180212059,2.66831522286306),
 .UNSPECIFIED.);
#1733=B_SPLINE_CURVE_WITH_KNOTS('',3,(#162532,#162533,#162534,#162535,#162536,
#162537,#162538,#162539,#162540,#162541,#162542,#162543,#162544),
 .UNSPECIFIED.,.F.,.F.,(4,3,3,3,4),(-48.1740291001457,-48.070804245227,
-47.9674104963029,-47.94414959817,-47.8233361836797),.UNSPECIFIED.);
#1734=B_SPLINE_CURVE_WITH_KNOTS('',3,(#162549,#162550,#162551,#162552,#162553,
#162554,#162555,#162556,#162557,#162558,#162559,#162560,#162561,#162562,
#162563,#162564,#162565,#162566,#162567,#162568,#162569,#162570,#162571,
#162572,#162573,#162574,#162575,#162576,#162577,#162578,#162579,#162580,
#162581,#162582,#162583,#162584,#162585,#162586,#162587,#162588,#162589,
#162590,#162591,#162592,#162593,#162594,#162595,#162596,#162597,#162598,
#162599,#162600,#162601,#162602,#162603,#162604,#162605,#162606,#162607,
#162608,#162609,#162610,#162611,#162612,#162613,#162614,#162615,#162616,
#162617,#162618,#162619,#162620,#162621,#162622,#162623,#162624,#162625,
#162626,#162627,#162628,#162629,#162630,#162631,#162632,#162633,#162634,
#162635,#162636,#162637,#162638,#162639,#162640,#162641,#162642,#162643,
#162644,#162645,#162646,#162647,#162648,#162649,#162650,#162651,#162652,
#162653,#162654,#162655,#162656,#162657,#162658,#162659,#162660,#162661,
#162662,#162663,#162664,#162665,#162666,#162667,#162668,#162669,#162670,
#162671,#162672,#162673,#162674,#162675,#162676,#162677,#162678,#162679,
#162680,#162681,#162682,#162683,#162684,#162685,#162686,#162687,#162688,
#162689,#162690,#162691,#162692,#162693,#162694,#162695,#162696,#162697,
#162698,#162699,#162700,#162701,#162702,#162703,#162704,#162705,#162706,
#162707,#162708,#162709,#162710,#162711,#162712,#162713,#162714,#162715,
#162716,#162717,#162718,#162719,#162720,#162721,#162722,#162723,#162724,
#162725,#162726,#162727,#162728,#162729,#162730,#162731,#162732,#162733,
#162734,#162735,#162736,#162737,#162738,#162739,#162740,#162741,#162742,
#162743,#162744,#162745,#162746,#162747,#162748,#162749,#162750,#162751,
#162752,#162753,#162754,#162755,#162756,#162757,#162758,#162759,#162760,
#162761,#162762,#162763,#162764,#162765,#162766,#162767,#162768,#162769,
#162770,#162771,#162772,#162773,#162774,#162775,#162776,#162777,#162778,
#162779,#162780),.UNSPECIFIED.,.F.,.F.,(4,2,2,2,2,2,2,2,2,2,2,2,2,2,2,2,
2,2,2,2,2,2,2,2,2,2,2,2,2,2,2,2,2,2,2,2,2,2,2,2,2,2,2,2,2,2,2,2,2,2,2,2,
2,2,2,2,2,2,2,2,2,2,2,2,2,2,2,2,2,2,2,2,2,2,2,2,2,2,2,2,2,2,2,2,2,2,2,2,
2,2,2,2,2,2,2,2,2,2,2,2,2,2,2,2,2,2,2,2,2,2,2,2,2,2,2,4),(1.25968344386625,
1.28150393949821,1.30395459826603,1.31433181789067,1.31654822237659,1.31779250816769,
1.31886523225317,1.32022982656628,1.32240323674052,1.33389993938574,1.38263554309166,
1.41583881962656,1.42010267369441,1.42263496489568,1.42457438527109,1.42665174044739,
1.42991805103097,1.440381112104,1.45728206404355,1.49511039169191,1.52518596249867,
1.52810055377774,1.52948933043945,1.5305643070714,1.53179242573215,1.53393535200595,
1.54323150792161,1.56207804948947,1.6024785251327,1.61474061934373,1.62934646323569,
1.63313474148773,1.63534973117589,1.63726199042886,1.63959702007219,1.64404694231465,
1.67495964457103,1.7218063003911,1.73760402139448,1.74021650558827,1.74156239028271,
1.74263375961614,1.74389194951601,1.74617206525345,1.75760864352059,1.78402404438808,
1.83638781280756,1.84332624544597,1.84620032318074,1.847994782719,1.84995539175352,
1.85265691075267,1.85904676502496,1.88738505136668,1.93728489306762,1.94991460954658,
1.95215085420973,1.95353447610928,1.95460898415596,1.95584052030327,1.95799872417219,
1.96750744967562,2.01664201563862,2.05182814883153,2.05612450854903,2.05866627047294,
2.06060727589271,2.06268082597604,2.06592963981941,2.0762388705972,2.09279804116576,
2.1256856002288,2.13955191023882,2.14611402275446,2.16166405363361,2.16426448434662,
2.16560772427733,2.16667887608442,2.16793900642414,2.17022826098598,2.18182902855897,
2.20890564652439,2.26033635833336,2.26733508487012,2.27021903465975,2.27201522785433,
2.27397419398567,2.27666700567814,2.28300614085763,2.31092468184607,2.3569364842496,
2.35799573600593,2.37367266475889,2.37627850051508,2.37762290532363,2.37869412496694,
2.37995333413688,2.38223835174115,2.39376346889887,2.42053434164097,2.47236736426887,
2.47935688017427,2.48223929524866,2.48403520171132,2.48585600442242,2.48840937961275,
2.49400406753632,2.50151762643898,2.52045156533893,2.54849914024973,2.58534459312385,
2.58818603325233,2.58956046783506,2.59063397996847,2.59187131574407,2.59333918514653),
 .UNSPECIFIED.);
#1735=B_SPLINE_CURVE_WITH_KNOTS('',3,(#162782,#162783,#162784,#162785,#162786,
#162787,#162788,#162789,#162790,#162791,#162792,#162793,#162794,#162795,
#162796,#162797,#162798,#162799,#162800,#162801,#162802,#162803,#162804,
#162805,#162806,#162807,#162808,#162809,#162810,#162811,#162812,#162813,
#162814,#162815,#162816,#162817,#162818,#162819,#162820,#162821,#162822,
#162823,#162824,#162825,#162826,#162827,#162828,#162829,#162830,#162831,
#162832,#162833,#162834,#162835,#162836,#162837,#162838,#162839,#162840,
#162841,#162842,#162843,#162844,#162845,#162846,#162847,#162848,#162849,
#162850,#162851,#162852,#162853,#162854,#162855,#162856,#162857,#162858,
#162859,#162860,#162861,#162862,#162863,#162864,#162865,#162866,#162867,
#162868,#162869,#162870,#162871,#162872,#162873,#162874,#162875,#162876,
#162877,#162878,#162879,#162880,#162881,#162882,#162883,#162884,#162885,
#162886,#162887,#162888,#162889,#162890,#162891,#162892,#162893,#162894,
#162895,#162896,#162897,#162898,#162899,#162900,#162901,#162902,#162903,
#162904,#162905,#162906,#162907,#162908,#162909,#162910,#162911,#162912,
#162913,#162914,#162915,#162916,#162917,#162918,#162919,#162920,#162921,
#162922,#162923,#162924,#162925,#162926,#162927,#162928,#162929,#162930,
#162931,#162932,#162933,#162934,#162935,#162936,#162937,#162938,#162939,
#162940,#162941,#162942,#162943,#162944,#162945,#162946,#162947,#162948,
#162949,#162950,#162951,#162952,#162953,#162954,#162955,#162956,#162957,
#162958,#162959),.UNSPECIFIED.,.F.,.F.,(4,3,3,3,3,3,3,3,3,3,3,3,3,3,3,3,
3,3,3,3,3,3,3,3,3,3,3,3,3,3,3,3,3,3,3,3,3,3,3,3,3,3,3,3,3,3,3,3,3,3,3,3,
3,3,3,3,3,3,3,4),(-54.1065214908593,-53.9371682979412,-53.8337735608933,
-53.7305322787782,-53.6274123133859,-53.5243577451769,-53.4213345368191,
-53.3183086941466,-53.2151759273684,-53.1119868359586,-53.0086148425769,
-52.9383318479794,-52.8349371109313,-52.7316958288162,-52.6285758634238,
-52.5255212952148,-52.4224980868569,-52.3194722441843,-52.2163394774061,
-52.1131503859961,-52.0097783926143,-51.9394953980175,-51.8361006609696,
-51.7328593788547,-51.6297394134624,-51.5266848452536,-51.4236616368959,
-51.3206357942235,-51.2175030274454,-51.1143139360357,-51.0109419426541,
-50.9406589480556,-50.8372642110076,-50.7340229288926,-50.6309029635003,
-50.5278483952914,-50.4248251869336,-50.3217993442611,-50.218666577483,
-50.1154774860731,-50.0121054926915,-49.9418224980937,-49.8384277610458,
-49.7351864789307,-49.6320665135385,-49.5290119453296,-49.4259887369718,
-49.3229628942993,-49.2198301275212,-49.1166410361114,-49.0132690427297,
-48.9429860481318,-48.8396205066898,-48.7363953136868,-48.6332762150803,
-48.5302290794512,-48.4271932051626,-48.324164639594,-48.2210652728402,
-48.1740291001457),.UNSPECIFIED.);
#1736=B_SPLINE_CURVE_WITH_KNOTS('',3,(#162960,#162961,#162962,#162963),
 .UNSPECIFIED.,.F.,.F.,(4,4),(-54.4565131158552,-54.1065275198801),
 .UNSPECIFIED.);
#1737=B_SPLINE_CURVE_WITH_KNOTS('',3,(#162969,#162970,#162971,#162972,#162973,
#162974,#162975,#162976,#162977,#162978,#162979,#162980,#162981,#162982,
#162983,#162984,#162985,#162986,#162987,#162988),.UNSPECIFIED.,.F.,.F.,
(4,2,2,2,2,2,2,2,2,4),(2.59334882414752,2.59907506457794,2.60333221459039,
2.60586227935457,2.60780101189424,2.60987862294918,2.61314742471985,2.6169507883377,
2.62421563735964,2.66784423020342),.UNSPECIFIED.);
#1738=B_SPLINE_CURVE_WITH_KNOTS('',3,(#162989,#162990,#162991,#162992,#162993,
#162994,#162995,#162996,#162997,#162998,#162999,#163000,#163001,#163002,
#163003,#163004,#163005,#163006,#163007,#163008,#163009,#163010,#163011,
#163012,#163013,#163014,#163015,#163016,#163017,#163018,#163019,#163020,
#163021,#163022,#163023,#163024,#163025,#163026,#163027,#163028,#163029,
#163030,#163031,#163032,#163033,#163034,#163035,#163036,#163037,#163038,
#163039,#163040,#163041,#163042,#163043,#163044,#163045,#163046,#163047,
#163048,#163049,#163050,#163051,#163052,#163053,#163054,#163055,#163056,
#163057,#163058,#163059,#163060,#163061,#163062,#163063,#163064,#163065,
#163066,#163067,#163068,#163069,#163070,#163071,#163072,#163073,#163074,
#163075,#163076,#163077,#163078,#163079,#163080,#163081,#163082,#163083,
#163084,#163085,#163086,#163087,#163088,#163089,#163090,#163091,#163092,
#163093,#163094,#163095,#163096,#163097,#163098,#163099,#163100,#163101,
#163102,#163103,#163104,#163105,#163106,#163107,#163108,#163109,#163110,
#163111,#163112,#163113,#163114,#163115,#163116,#163117,#163118,#163119,
#163120,#163121,#163122,#163123,#163124,#163125,#163126,#163127,#163128,
#163129,#163130,#163131,#163132,#163133,#163134,#163135,#163136,#163137,
#163138,#163139,#163140,#163141,#163142,#163143,#163144,#163145,#163146,
#163147,#163148,#163149,#163150,#163151,#163152,#163153,#163154,#163155,
#163156,#163157,#163158,#163159,#163160,#163161,#163162,#163163,#163164,
#163165,#163166,#163167,#163168,#163169,#163170,#163171,#163172,#163173,
#163174,#163175,#163176,#163177,#163178,#163179,#163180,#163181,#163182,
#163183,#163184,#163185,#163186,#163187,#163188,#163189,#163190,#163191,
#163192,#163193,#163194,#163195,#163196,#163197,#163198,#163199,#163200,
#163201,#163202),.UNSPECIFIED.,.F.,.F.,(4,2,2,2,2,2,2,2,2,2,2,2,2,2,2,2,
2,2,2,2,2,2,2,2,2,2,2,2,2,2,2,2,2,2,2,2,2,2,2,2,2,2,2,2,2,2,2,2,2,2,2,2,
2,2,2,2,2,2,2,2,2,2,2,2,2,2,2,2,2,2,2,2,2,2,2,2,2,2,2,2,2,2,2,2,2,2,2,2,
2,2,2,2,2,2,2,2,2,2,2,2,2,2,2,2,2,2,4),(0.000649988335642877,0.0375152704990541,
0.0412926024578486,0.0433020294432964,0.0446072108356044,0.0458444142180878,
0.0469177266873797,0.0482917858053277,0.0511320544688072,0.0879796920395742,
0.109399124786516,0.136182092967779,0.146436026521021,0.149706920435959,
0.15178501628728,0.153723612827992,0.156252658605983,0.16050625487588,0.193185552789801,
0.222555354354387,0.244174106165292,0.254295247008305,0.256485228349918,
0.25773337791172,0.258805379538652,0.260163839407445,0.262835887780087,
0.280216640231541,0.329255233688801,0.347302837500602,0.354572268411801,
0.360002060810804,0.36256744550423,0.364504808798455,0.366332959206393,
0.368880882447617,0.375561602311507,0.430977353873264,0.455320875693043,
0.466218627605919,0.468466956050601,0.469718065506778,0.470789816457095,
0.472144378813639,0.47488629622175,0.493335007454673,0.537461269541001,
0.565331974112842,0.571665382296963,0.574357002609424,0.576315561046172,
0.578111702417444,0.580996264298724,0.58800001788294,0.639383010169877,
0.666515187811272,0.678128410926827,0.680418181092506,0.681678325206265,
0.682749329532794,0.684092177014792,0.686691244963384,0.702216369315421,
0.708761471480629,0.722633921401398,0.755493983493896,0.77205648267286,
0.782367905406938,0.785616709426293,0.787690091313945,0.789630826090766,
0.792172071500364,0.79646722690795,0.831578348115309,0.880465471459157,
0.890288659601052,0.892468517871547,0.893704749634407,0.89477845082597,
0.896154615331692,0.899004743368698,0.935374677289219,0.989163075558435,
0.995619128476982,0.998331696209567,1.00029419032283,1.00208616374467,1.00494709012616,
1.01180636960978,1.06524497318811,1.090935227857,1.10218662724822,1.10445604494005,
1.10571185352532,1.10678333809307,1.10813209108801,1.110758156089,1.12692234086465,
1.17758033537424,1.2019943210918,1.20789434186422,1.21051040626931,1.21245610456172,
1.21427050097894,1.21676510975846,1.22311495397694,1.25968344386625),
 .UNSPECIFIED.);
#1739=B_SPLINE_CURVE_WITH_KNOTS('',3,(#163204,#163205,#163206,#163207,#163208,
#163209,#163210,#163211,#163212,#163213),.UNSPECIFIED.,.F.,.F.,(4,1,1,1,
1,1,1,4),(-60.3897037700897,-59.9301869977125,-58.9313505477506,-57.9325140977887,
-56.9336776478269,-55.934841197865,-54.9360047479031,-54.4565131158552),
 .UNSPECIFIED.);
#1740=B_SPLINE_CURVE_WITH_KNOTS('',3,(#163214,#163215,#163216,#163217,#163218,
#163219,#163220,#163221,#163222,#163223,#163224,#163225,#163226,#163227,
#163228,#163229,#163230,#163231),.UNSPECIFIED.,.F.,.F.,(4,2,2,2,2,2,2,2,
4),(0.000658789415650989,0.00332970172644197,0.0059216589075676,0.00778879691858933,
0.00964368950037614,0.0114909185893229,0.0146445375726767,0.0233614964880355,
0.0750722492145438),.UNSPECIFIED.);
#1741=B_SPLINE_CURVE_WITH_KNOTS('',3,(#163236,#163237,#163238,#163239,#163240,
#163241,#163242,#163243,#163244,#163245,#163246,#163247,#163248,#163249,
#163250,#163251,#163252,#163253,#163254,#163255,#163256,#163257,#163258,
#163259,#163260,#163261,#163262,#163263,#163264,#163265,#163266,#163267,
#163268,#163269,#163270,#163271,#163272,#163273,#163274,#163275,#163276,
#163277,#163278,#163279,#163280,#163281,#163282,#163283,#163284,#163285,
#163286,#163287,#163288,#163289,#163290,#163291,#163292,#163293,#163294,
#163295,#163296,#163297,#163298,#163299,#163300,#163301,#163302,#163303,
#163304,#163305,#163306,#163307,#163308,#163309,#163310,#163311,#163312,
#163313,#163314,#163315,#163316,#163317,#163318,#163319,#163320,#163321,
#163322,#163323,#163324,#163325,#163326,#163327,#163328,#163329,#163330,
#163331,#163332,#163333,#163334,#163335,#163336,#163337,#163338,#163339,
#163340,#163341,#163342,#163343,#163344,#163345,#163346,#163347,#163348,
#163349,#163350,#163351,#163352,#163353,#163354,#163355,#163356,#163357,
#163358,#163359,#163360,#163361,#163362,#163363,#163364,#163365,#163366,
#163367,#163368,#163369,#163370,#163371,#163372,#163373,#163374,#163375,
#163376,#163377,#163378,#163379,#163380,#163381,#163382,#163383,#163384,
#163385,#163386,#163387,#163388,#163389,#163390,#163391,#163392,#163393,
#163394,#163395,#163396,#163397,#163398,#163399,#163400,#163401,#163402,
#163403,#163404,#163405,#163406,#163407,#163408,#163409,#163410,#163411,
#163412,#163413,#163414,#163415,#163416,#163417,#163418,#163419,#163420,
#163421,#163422,#163423,#163424,#163425,#163426,#163427,#163428,#163429,
#163430,#163431,#163432,#163433,#163434,#163435,#163436,#163437,#163438,
#163439,#163440,#163441,#163442,#163443,#163444,#163445,#163446,#163447,
#163448,#163449,#163450,#163451,#163452,#163453,#163454,#163455,#163456,
#163457),.UNSPECIFIED.,.F.,.F.,(4,2,2,2,2,2,2,2,2,2,2,2,2,2,2,2,2,2,2,2,
2,2,2,2,2,2,2,2,2,2,2,2,2,2,2,2,2,2,2,2,2,2,2,2,2,2,2,2,2,2,2,2,2,2,2,2,
2,2,2,2,2,2,2,2,2,2,2,2,2,2,2,2,2,2,2,2,2,2,2,2,2,2,2,2,2,2,2,2,2,2,2,2,
2,2,2,2,2,2,2,2,2,2,2,2,2,2,2,2,2,2,4),(1.25996006495675,1.28597380944536,
1.32674485088401,1.33181142606065,1.33427121096303,1.33619431271336,1.33832607326192,
1.34183902862498,1.35471582196281,1.37741958663076,1.41601236368063,1.42100702049356,
1.43701511615223,1.439634657082,1.44098193712491,1.44205323813183,1.44330998086227,
1.44558399481097,1.45691813035294,1.48293120542186,1.53585432794066,1.54275018415212,
1.54561697653284,1.54740990675929,1.54937126959613,1.55207826794206,1.55850204924136,
1.58712802854869,1.6384137574983,1.64947627869533,1.65162341522331,1.65297992887205,
1.65405190176624,1.65530175680869,1.65754404067806,1.6683401259638,1.69230181102095,
1.7482595273408,1.75488535343838,1.75742482539986,1.75925083788514,1.76118954825343,
1.7637628543973,1.76942781234478,1.79207264981186,1.82489292604725,1.82936666735762,
1.86060995899561,1.86352206217553,1.86491022324517,1.86598498575407,1.86721315325864,
1.86935685212576,1.87866697764114,1.92781063757243,1.96318650993906,1.96748434638255,
1.97002624300663,1.97196692592091,1.97403971921933,1.97728648697316,1.98758198063248,
2.00411220184513,2.03697136145416,2.0485222492667,2.0580882762403,2.07304463335334,
2.07539212821845,2.07679360363977,2.0778727343703,2.07907911818313,2.08112476943751,
2.08918051648865,2.10435470460193,2.14436455266355,2.17524266362502,2.17945964517444,
2.18197798267303,2.18391481249275,2.18599733515636,2.18928858714235,2.19997838021427,
2.21739013031273,2.25491166888488,2.28448034825575,2.28739436561197,2.2887828350069,
2.28985755825139,2.29108537004048,2.29322772015703,2.30252074880178,2.32135992475989,
2.3691444305163,2.38804715265221,2.39179672343498,2.39420162815337,2.39611860978283,
2.39828237714473,2.40194076057161,2.41628811257928,2.46674887119079,2.49644856364972,
2.49936273260099,2.50075125350221,2.50182600707965,2.50305384286103,2.50434565237812,
2.50899003897626,2.53312554767631,2.55402964662815,2.59334882414752),
 .UNSPECIFIED.);
#1742=B_SPLINE_CURVE_WITH_KNOTS('',3,(#163458,#163459,#163460,#163461,#163462,
#163463,#163464,#163465,#163466,#163467,#163468,#163469,#163470,#163471,
#163472,#163473,#163474,#163475,#163476,#163477,#163478,#163479,#163480,
#163481,#163482,#163483,#163484,#163485,#163486,#163487,#163488,#163489,
#163490,#163491,#163492,#163493,#163494,#163495,#163496,#163497,#163498,
#163499,#163500,#163501,#163502,#163503,#163504,#163505,#163506,#163507,
#163508,#163509,#163510,#163511,#163512,#163513,#163514,#163515,#163516,
#163517,#163518,#163519,#163520,#163521,#163522,#163523,#163524,#163525,
#163526,#163527,#163528,#163529,#163530,#163531,#163532,#163533,#163534,
#163535,#163536,#163537,#163538,#163539,#163540,#163541,#163542,#163543,
#163544,#163545,#163546,#163547,#163548,#163549,#163550,#163551,#163552,
#163553,#163554,#163555,#163556,#163557,#163558,#163559,#163560,#163561,
#163562,#163563,#163564,#163565,#163566,#163567,#163568,#163569,#163570,
#163571,#163572,#163573,#163574,#163575,#163576,#163577,#163578,#163579,
#163580,#163581,#163582,#163583,#163584,#163585,#163586,#163587,#163588,
#163589,#163590,#163591,#163592,#163593,#163594,#163595,#163596,#163597,
#163598,#163599,#163600,#163601,#163602,#163603,#163604,#163605,#163606,
#163607,#163608,#163609,#163610,#163611,#163612,#163613,#163614,#163615,
#163616,#163617,#163618,#163619,#163620,#163621,#163622,#163623,#163624,
#163625,#163626,#163627,#163628,#163629,#163630,#163631,#163632,#163633,
#163634,#163635,#163636,#163637,#163638,#163639,#163640,#163641,#163642,
#163643,#163644,#163645,#163646,#163647,#163648,#163649,#163650,#163651,
#163652,#163653,#163654,#163655,#163656,#163657,#163658,#163659,#163660,
#163661,#163662,#163663,#163664,#163665,#163666,#163667,#163668,#163669,
#163670,#163671,#163672,#163673,#163674,#163675,#163676,#163677,#163678,
#163679,#163680,#163681,#163682,#163683,#163684,#163685,#163686,#163687,
#163688,#163689),.UNSPECIFIED.,.F.,.F.,(4,2,2,2,2,2,2,2,2,2,2,2,2,2,2,2,
2,2,2,2,2,2,2,2,2,2,2,2,2,2,2,2,2,2,2,2,2,2,2,2,2,2,2,2,2,2,2,2,2,2,2,2,
2,2,2,2,2,2,2,2,2,2,2,2,2,2,2,2,2,2,2,2,2,2,2,2,2,2,2,2,2,2,2,2,2,2,2,2,
2,2,2,2,2,2,2,2,2,2,2,2,2,2,2,2,2,2,2,2,2,2,2,2,2,2,2,4),(0.0750722492145438,
0.089273883774724,0.108736238450361,0.112675312821005,0.114244472673274,
0.115347616226248,0.116358705151943,0.118025380652166,0.122269071395783,
0.177793694177577,0.20980237985404,0.214435981151818,0.217207823473553,
0.219715316432243,0.221616785883321,0.223439946924427,0.225968447943757,
0.23252618265342,0.289135495830322,0.312706921624991,0.323396188599504,
0.325632024315669,0.326880500483277,0.327952665500023,0.329311181849471,
0.331982887691663,0.349344799089393,0.367622576687107,0.400551307754336,
0.417194792829087,0.427543042342775,0.430796238022716,0.432870694703231,
0.434811223168959,0.437350451056223,0.441638284565254,0.476878520823009,
0.526123759127554,0.535534348299561,0.537685601829783,0.53891560030055,
0.539990347196359,0.541376346694768,0.544276404838197,0.571047910819831,
0.604901022440056,0.634235374311171,0.640744266195993,0.643465965726574,
0.645430367194715,0.647220865877107,0.650072482212639,0.656873699709213,
0.711030798235968,0.736238318680125,0.747365576963437,0.749628025633159,
0.750882442839031,0.751954244112297,0.753305315181373,0.755941569721024,
0.772353473841486,0.822423716415776,0.840492796456449,0.85147298973827,
0.854796816312565,0.856886996706432,0.858822060696727,0.861325554531746,
0.86549026163651,0.894122056722588,0.947186140854307,0.959329892388681,
0.961648912215588,0.962915634525559,0.963986564537474,0.965322182956684,
0.967400428234967,0.977395418297254,0.98298968078243,0.992387406060152,
1.00395842269926,1.0368083948603,1.05335110980195,1.06365451181599,1.06690307695976,
1.06897685660727,1.07091835030893,1.0734611474474,1.07776017657869,1.11307373987275,
1.16233282766085,1.17167136585897,1.17381782426907,1.17504695403105,1.17612216086331,
1.1775103606059,1.1804206757723,1.20855458469213,1.24824747237768,1.26519455449022,
1.27568027571575,1.27894981726275,1.28102832364675,1.28296818879352,1.28550015870478,
1.28976149589151,1.33476567404375,1.379821053785,1.38454671693276,1.3862891876652,
1.38731528140148,1.38840808509425,1.38991874143622,1.39350070371916,1.40892859190044),
 .UNSPECIFIED.);
#1743=B_SPLINE_CURVE_WITH_KNOTS('',3,(#163695,#163696,#163697,#163698,#163699),
 .UNSPECIFIED.,.F.,.F.,(4,1,4),(76.7075601022117,76.9104066470643,77.0584304498949),
 .UNSPECIFIED.);
#1744=B_SPLINE_CURVE_WITH_KNOTS('',3,(#163700,#163701,#163702,#163703,#163704,
#163705,#163706,#163707,#163708,#163709,#163710,#163711,#163712,#163713,
#163714,#163715,#163716,#163717,#163718,#163719,#163720,#163721,#163722,
#163723,#163724,#163725,#163726,#163727,#163728,#163729,#163730,#163731,
#163732,#163733,#163734,#163735,#163736,#163737,#163738,#163739,#163740,
#163741,#163742,#163743,#163744,#163745,#163746,#163747,#163748,#163749,
#163750,#163751,#163752,#163753,#163754,#163755,#163756,#163757,#163758,
#163759,#163760,#163761,#163762,#163763,#163764,#163765,#163766,#163767,
#163768,#163769,#163770,#163771,#163772,#163773,#163774,#163775,#163776,
#163777,#163778,#163779,#163780,#163781,#163782,#163783,#163784,#163785,
#163786,#163787,#163788,#163789,#163790,#163791,#163792,#163793,#163794,
#163795,#163796,#163797,#163798,#163799,#163800,#163801,#163802,#163803,
#163804,#163805,#163806,#163807,#163808,#163809,#163810,#163811,#163812,
#163813,#163814,#163815,#163816,#163817,#163818,#163819,#163820,#163821,
#163822,#163823,#163824,#163825,#163826,#163827,#163828,#163829,#163830,
#163831,#163832,#163833,#163834,#163835,#163836,#163837,#163838,#163839,
#163840,#163841,#163842,#163843,#163844,#163845,#163846,#163847,#163848,
#163849,#163850,#163851,#163852,#163853,#163854,#163855,#163856,#163857,
#163858,#163859,#163860,#163861,#163862,#163863,#163864,#163865,#163866,
#163867,#163868,#163869,#163870,#163871,#163872,#163873,#163874,#163875,
#163876,#163877,#163878,#163879,#163880,#163881,#163882,#163883,#163884,
#163885,#163886,#163887,#163888,#163889,#163890,#163891,#163892,#163893,
#163894,#163895,#163896,#163897,#163898,#163899,#163900,#163901,#163902,
#163903,#163904,#163905,#163906,#163907,#163908,#163909,#163910,#163911,
#163912,#163913,#163914,#163915,#163916,#163917,#163918,#163919),
 .UNSPECIFIED.,.F.,.F.,(4,2,2,2,2,2,2,2,2,2,2,2,2,2,2,2,2,2,2,2,2,2,2,2,
2,2,2,2,2,2,2,2,2,2,2,2,2,2,2,2,2,2,2,2,2,2,2,2,2,2,2,2,2,2,2,2,2,2,2,2,
2,2,2,2,2,2,2,2,2,2,2,2,2,2,2,2,2,2,2,2,2,2,2,2,2,2,2,2,2,2,2,2,2,2,2,2,
2,2,2,2,2,2,2,2,2,2,2,2,2,4),(0.000629226549544607,0.046842092175668,0.0541657575285493,
0.0579911612059392,0.0612752544363508,0.0633561305284231,0.0652934283883815,
0.0678152242493139,0.0720443245894624,0.118700329279881,0.138793897037419,
0.156963094474695,0.166022017532338,0.168062688078218,0.169315730423518,
0.1703871574697,0.171738779642116,0.174379144044047,0.190917543624233,0.199764859285149,
0.243742949382162,0.259907590363103,0.269996325263167,0.273243717522023,
0.27531653418407,0.277256975786934,0.279798177711421,0.284094022729987,
0.319313332422387,0.368562126872632,0.377950976793733,0.38010027972992,
0.381329644954602,0.382404151719005,0.383790254026362,0.386035372754029,
0.398844428626804,0.401655625631889,0.40593911242359,0.448927943809981,
0.47686676063002,0.483208308591596,0.485901261068954,0.487860007173649,
0.48965577917277,0.49253855924609,0.499531921315542,0.551066850555209,0.578088456860946,
0.589674282153311,0.591962469797789,0.593222244789865,0.594293237545087,
0.595636453608052,0.598237350724384,0.61380689768479,0.620262240882701,
0.661679829577953,0.688953552007046,0.695214266325076,0.697893453563024,
0.699849814058667,0.70164870862721,0.704548219403095,0.711641621297567,
0.761302991780524,0.799617001575597,0.803221546299077,0.804735597480476,
0.805828574784582,0.806853018956235,0.808588829136208,0.813273992121576,
0.854358207744742,0.900791019632297,0.907183313454101,0.909885000778856,
0.911845419513227,0.913639493175818,0.916512478861638,0.923445809804724,
0.975895767454485,1.00227120613405,1.01369641930391,1.01597568328913,1.01723357649087,
1.01830480150809,1.01965063653427,1.02226341151027,1.03811575328452,1.0428600613946,
1.05813888688782,1.09101631580087,1.10759893567686,1.11791955846622,1.12116949240115,
1.12324317073249,1.12518388478307,1.12772467291816,1.13201809166524,1.17442090269835,
1.20348006573086,1.22309714942415,1.22705256328181,1.22862432579257,1.22972797012696,
1.2307384947667,1.2324022084367,1.2366275620297,1.25996006495675),
 .UNSPECIFIED.);
#1745=B_SPLINE_CURVE_WITH_KNOTS('',3,(#163921,#163922,#163923,#163924,#163925,
#163926,#163927,#163928,#163929,#163930,#163931,#163932,#163933,#163934,
#163935,#163936,#163937,#163938,#163939,#163940,#163941,#163942,#163943,
#163944,#163945,#163946,#163947,#163948,#163949,#163950,#163951,#163952,
#163953,#163954,#163955,#163956,#163957,#163958,#163959,#163960,#163961,
#163962,#163963,#163964,#163965,#163966,#163967,#163968,#163969,#163970,
#163971,#163972,#163973,#163974,#163975,#163976,#163977,#163978,#163979,
#163980,#163981,#163982,#163983,#163984,#163985,#163986,#163987,#163988,
#163989,#163990,#163991,#163992,#163993,#163994,#163995,#163996,#163997,
#163998,#163999,#164000,#164001,#164002,#164003,#164004,#164005,#164006,
#164007,#164008,#164009,#164010,#164011,#164012,#164013,#164014,#164015,
#164016,#164017,#164018,#164019,#164020,#164021,#164022,#164023,#164024,
#164025,#164026,#164027,#164028,#164029,#164030,#164031,#164032,#164033,
#164034,#164035,#164036,#164037,#164038,#164039,#164040,#164041,#164042,
#164043,#164044,#164045,#164046,#164047,#164048,#164049,#164050,#164051,
#164052,#164053,#164054,#164055,#164056,#164057,#164058,#164059,#164060,
#164061,#164062,#164063,#164064,#164065,#164066,#164067,#164068,#164069,
#164070,#164071,#164072,#164073,#164074,#164075,#164076,#164077,#164078,
#164079,#164080,#164081,#164082,#164083,#164084,#164085,#164086,#164087,
#164088,#164089,#164090,#164091,#164092,#164093,#164094,#164095,#164096,
#164097,#164098,#164099,#164100,#164101,#164102,#164103,#164104,#164105,
#164106,#164107,#164108,#164109,#164110,#164111,#164112,#164113,#164114,
#164115,#164116,#164117,#164118,#164119,#164120,#164121,#164122,#164123,
#164124,#164125,#164126,#164127,#164128,#164129,#164130,#164131,#164132,
#164133,#164134,#164135,#164136,#164137,#164138,#164139,#164140,#164141,
#164142,#164143,#164144,#164145,#164146),.UNSPECIFIED.,.F.,.F.,(4,2,2,2,
2,2,2,2,2,2,2,2,2,2,2,2,2,2,2,2,2,2,2,2,2,2,2,2,2,2,2,2,2,2,2,2,2,2,2,2,
2,2,2,2,2,2,2,2,2,2,2,2,2,2,2,2,2,2,2,2,2,2,2,2,2,2,2,2,2,2,2,2,2,2,2,2,
2,2,2,2,2,2,2,2,2,2,2,2,2,2,2,2,2,2,2,2,2,2,2,2,2,2,2,2,2,2,2,2,2,2,2,2,
4),(1.40892859190044,1.43114189525,1.48156963760009,1.48862884966623,1.49152354603348,
1.49332221530073,1.49528052898801,1.49796636219948,1.50426089205288,1.5318023820529,
1.56020878468567,1.58254081662385,1.59524891900965,1.59748968510969,1.59887485677546,
1.59994976947127,1.60118087293459,1.60333620221715,1.61279870529294,1.66198861182054,
1.69719664481167,1.70149430577838,1.70403678888311,1.70597831701588,1.70805239834854,
1.71130198785045,1.721613202209,1.73817510452622,1.77107000802575,1.78480619463583,
1.79167956450897,1.79189418137142,1.79536650019118,1.80737171117298,1.80957450844001,
1.81094817097448,1.81202190509395,1.81326043127816,1.81544975243714,1.825407228245,
1.87417264068421,1.90924350060804,1.91353909054562,1.91608088179307,1.91802218880617,
1.92009633181582,1.92334664001236,1.93366537978797,1.95024436120885,1.98315211084013,
1.99823835888684,2.0031473962221,2.01907406400683,2.02168979752071,2.0230364933786,
2.02410805362961,2.02536594006684,2.02764416092539,2.03904333943293,2.06530752573197,
2.11789890057591,2.12482260230917,2.12769449841476,2.1294887402672,2.13145002916269,
2.13415416338517,2.14055810834717,2.1493891515329,2.20069624065193,2.23073837411376,
2.23364986311164,2.23503820339814,2.23611332207084,2.2373421398203,2.23948754375142,
2.24881389940775,2.29801565533926,2.33335075691658,2.33764950756903,2.34019213947976,
2.34213349578752,2.34420711688365,2.34745540783189,2.35775763847839,2.37430048861872,
2.40717708608884,2.44285422472894,2.44571910689232,2.44709832297037,2.4481380605453,
2.44933265324992,2.45060555987713,2.45253662007598,2.4561069498846,2.46455680718911,
2.52380836385539,2.54607880918444,2.55001381715811,2.55247565713357,2.55439930196016,
2.55653057598231,2.56004021933743,2.57287658598738,2.5954737366041,2.64831919803709,
2.65619097239154,2.65828700262456,2.65951699757958,2.66057382320596,2.66161973450024,
2.66297018535776,2.66542827555432,2.66852198484313),.UNSPECIFIED.);
#1746=B_SPLINE_CURVE_WITH_KNOTS('',3,(#164147,#164148,#164149,#164150,#164151,
#164152),.UNSPECIFIED.,.F.,.F.,(4,2,4),(0.000817339722073156,0.0612254310813656,
0.0752219538553924),.UNSPECIFIED.);
#1747=B_SPLINE_CURVE_WITH_KNOTS('',3,(#164158,#164159,#164160,#164161,#164162,
#164163,#164164,#164165,#164166,#164167,#164168,#164169,#164170),
 .UNSPECIFIED.,.F.,.F.,(4,3,3,3,4),(82.9907456874083,83.0928761471772,83.1948834239356,
83.2967928187794,83.3413405014001),.UNSPECIFIED.);
#1748=B_SPLINE_CURVE_WITH_KNOTS('',3,(#164171,#164172,#164173,#164174,#164175,
#164176,#164177,#164178,#164179,#164180),.UNSPECIFIED.,.F.,.F.,(4,1,1,1,
1,1,1,4),(77.0584304498949,77.9092430970262,78.9080795469881,79.90691599695,
80.9057524469118,81.9045888968737,82.9034253468356,82.9907454093913),
 .UNSPECIFIED.);
#1749=B_SPLINE_CURVE_WITH_KNOTS('',3,(#164181,#164182,#164183,#164184,#164185,
#164186,#164187,#164188,#164189,#164190,#164191,#164192,#164193,#164194,
#164195,#164196,#164197,#164198,#164199,#164200,#164201,#164202,#164203,
#164204,#164205,#164206,#164207,#164208,#164209,#164210,#164211,#164212,
#164213,#164214,#164215,#164216,#164217,#164218,#164219,#164220,#164221,
#164222,#164223,#164224,#164225,#164226,#164227,#164228,#164229,#164230,
#164231,#164232,#164233,#164234,#164235,#164236,#164237,#164238,#164239,
#164240,#164241,#164242,#164243,#164244,#164245,#164246,#164247,#164248,
#164249,#164250,#164251,#164252,#164253,#164254,#164255,#164256,#164257,
#164258,#164259,#164260,#164261,#164262,#164263,#164264,#164265,#164266,
#164267,#164268,#164269,#164270,#164271,#164272,#164273,#164274,#164275,
#164276,#164277,#164278,#164279,#164280,#164281,#164282,#164283,#164284,
#164285,#164286,#164287,#164288,#164289,#164290,#164291,#164292,#164293,
#164294,#164295,#164296,#164297,#164298,#164299,#164300,#164301,#164302,
#164303,#164304,#164305,#164306,#164307,#164308,#164309,#164310,#164311,
#164312,#164313,#164314,#164315,#164316,#164317,#164318,#164319,#164320,
#164321,#164322,#164323,#164324,#164325,#164326,#164327,#164328,#164329,
#164330,#164331,#164332,#164333,#164334,#164335,#164336,#164337,#164338,
#164339,#164340,#164341,#164342,#164343,#164344,#164345,#164346,#164347,
#164348,#164349,#164350,#164351,#164352,#164353,#164354,#164355,#164356,
#164357,#164358,#164359,#164360,#164361,#164362,#164363,#164364,#164365,
#164366,#164367,#164368,#164369,#164370,#164371,#164372,#164373,#164374,
#164375,#164376,#164377,#164378,#164379,#164380,#164381,#164382,#164383,
#164384,#164385,#164386,#164387,#164388,#164389,#164390,#164391,#164392,
#164393,#164394,#164395,#164396,#164397,#164398,#164399,#164400,#164401,
#164402,#164403,#164404,#164405,#164406,#164407,#164408,#164409,#164410,
#164411,#164412,#164413,#164414,#164415,#164416,#164417,#164418,#164419,
#164420,#164421,#164422,#164423,#164424,#164425,#164426,#164427,#164428,
#164429,#164430,#164431,#164432,#164433,#164434,#164435,#164436,#164437,
#164438,#164439,#164440,#164441,#164442,#164443,#164444,#164445,#164446,
#164447,#164448,#164449,#164450,#164451,#164452),.UNSPECIFIED.,.F.,.F.,
(4,2,2,2,2,2,2,2,2,2,2,2,2,2,2,2,2,2,2,2,2,2,2,2,2,2,2,2,2,2,2,2,2,2,2,
2,2,2,2,2,2,2,2,2,2,2,2,2,2,2,2,2,2,2,2,2,2,2,2,2,2,2,2,2,2,2,2,2,2,2,2,
2,2,2,2,2,2,2,2,2,2,2,2,2,2,2,2,2,2,2,2,2,2,2,2,2,2,2,2,2,2,2,2,2,2,2,2,
2,2,2,2,2,2,2,2,2,2,2,2,2,2,2,2,2,2,2,2,2,2,2,2,2,2,2,2,4),(0.0752219538553924,
0.0876737708541335,0.0938318742109832,0.0964929811556149,0.0984458548898336,
0.100248360570854,0.103168886737211,0.110389679589265,0.154249340375915,
0.195394743117652,0.199213037433027,0.201237853233969,0.202549373332438,
0.203773000142621,0.203776566961232,0.20378014633625,0.203783738344437,
0.203787576062818,0.203791475620769,0.203795438321307,0.203799465536059,
0.203803558471933,0.203807718709299,0.203811947684853,0.203816246902364,
0.203820618031701,0.203825062595836,0.20382958214438,0.203834178495644,
0.20383885333795,0.203843608503851,0.203848445798754,0.204892188634865,
0.206274906167045,0.209159727727915,0.243329463902013,0.277571728409199,
0.294126608529013,0.304434011130635,0.307681933460342,0.309754845148587,
0.311695204779934,0.314236052710389,0.318530746432302,0.353665860888674,
0.402638504555908,0.412346629803975,0.414518311734997,0.415752592306471,
0.416826320029807,0.418204770135486,0.421067385718614,0.45674511001175,
0.48957118273493,0.506095244510139,0.516388962923495,0.519635506027736,
0.521708242933433,0.523648934759903,0.526190933368832,0.530489176948989,
0.565878123660799,0.615047144328223,0.624359823472386,0.626503768937628,
0.627732011539939,0.628806801992257,0.630194938639619,0.633106794523024,
0.664374889134527,0.698027864840962,0.716835852182718,0.728133512349959,
0.731490771685652,0.733588042679064,0.735520217769766,0.738006767535329,
0.742114736855211,0.76858503955736,0.82369449053593,0.836025073979104,0.838353481940201,
0.839622072387379,0.840692655893767,0.842025423707611,0.844094869680189,
0.853967703999288,0.859546786547861,0.8599910416698,0.866878668556703,0.880605864107274,
0.913468555540373,0.930031312953361,0.940343208578569,0.943592327683018,
0.945665950564827,0.947606938949967,0.950148556885713,0.954444432580003,
0.989573379916252,1.03850731938857,1.04828346516449,1.05046030904877,1.05169597405116,
1.05276991396152,1.05414733960082,1.05700336173895,1.07978617932669,1.09263096531517,
1.12548858440065,1.14204277479925,1.15235109418109,1.15560002206625,1.15767374778362,
1.15961499040838,1.16215716922543,1.16645450396551,1.20166389770812,1.25084883176782,
1.26033868215133,1.26249578897222,1.26372719167067,1.26480190722889,1.26618621191743,
1.26907693598538,1.29478181286462,1.33423137066986,1.36195679610043,1.36609770007442,
1.36859435658635,1.37052854731926,1.37262217691922,1.37596096942245,1.38707796583593,
1.40546485002873,1.40868741081837),.UNSPECIFIED.);
#1750=B_SPLINE_CURVE_WITH_KNOTS('',3,(#164458,#164459,#164460,#164461,#164462,
#164463,#164464,#164465,#164466,#164467,#164468,#164469,#164470,#164471,
#164472,#164473,#164474,#164475,#164476,#164477,#164478,#164479,#164480,
#164481,#164482,#164483),.UNSPECIFIED.,.F.,.F.,(4,2,2,2,2,2,2,2,2,2,2,2,
4),(2.59401617871736,2.61331896027604,2.62543797507626,2.62726567564924,
2.62826739459209,2.63695713257526,2.64010895985652,2.64195641923086,2.64381178633705,
2.64568025361034,2.64808223741416,2.65182298569027,2.66845987342429),
 .UNSPECIFIED.);
#1751=B_SPLINE_CURVE_WITH_KNOTS('',3,(#164484,#164485,#164486,#164487,#164488,
#164489,#164490,#164491,#164492,#164493,#164494,#164495,#164496,#164497,
#164498,#164499,#164500,#164501,#164502,#164503,#164504,#164505,#164506,
#164507,#164508,#164509,#164510,#164511,#164512,#164513,#164514,#164515,
#164516,#164517,#164518,#164519,#164520,#164521,#164522,#164523,#164524,
#164525,#164526,#164527,#164528,#164529,#164530,#164531,#164532,#164533,
#164534,#164535,#164536,#164537,#164538,#164539,#164540,#164541,#164542,
#164543,#164544,#164545,#164546,#164547,#164548,#164549,#164550,#164551,
#164552,#164553,#164554,#164555,#164556,#164557,#164558,#164559,#164560,
#164561,#164562,#164563,#164564,#164565,#164566,#164567,#164568,#164569,
#164570,#164571,#164572,#164573,#164574,#164575,#164576,#164577,#164578,
#164579,#164580,#164581,#164582,#164583,#164584,#164585,#164586,#164587,
#164588,#164589,#164590,#164591,#164592,#164593,#164594,#164595,#164596,
#164597,#164598,#164599,#164600,#164601,#164602,#164603,#164604,#164605,
#164606,#164607,#164608,#164609,#164610,#164611,#164612,#164613,#164614,
#164615,#164616,#164617,#164618,#164619,#164620,#164621,#164622,#164623,
#164624,#164625,#164626,#164627,#164628,#164629,#164630,#164631,#164632,
#164633,#164634,#164635,#164636,#164637,#164638,#164639,#164640,#164641,
#164642,#164643,#164644,#164645,#164646,#164647,#164648,#164649,#164650,
#164651,#164652,#164653,#164654,#164655,#164656,#164657,#164658,#164659,
#164660,#164661,#164662,#164663,#164664),.UNSPECIFIED.,.F.,.F.,(4,3,3,3,
3,3,3,3,3,3,3,3,3,3,3,3,3,3,3,3,3,3,3,3,3,3,3,3,3,3,3,3,3,3,3,3,3,3,3,3,
3,3,3,3,3,3,3,3,3,3,3,3,3,3,3,3,3,3,3,3,4),(83.3413405014001,83.4431911867645,
83.5450420715455,83.6469949427505,83.7490047344159,83.8511878793355,83.9022617967974,
84.0056565338454,84.1088978159603,84.2120177813527,84.3150723495616,84.4180955579194,
84.521121400592,84.6242541673701,84.7274432587799,84.8308152521616,84.9010982467593,
85.0044929838071,85.1077342659222,85.2108542313145,85.3139087995234,85.4169320078811,
85.5199578505539,85.6230906173319,85.7262797087418,85.8296517021234,85.8999346967212,
86.0033294337692,86.1065707158841,86.2096906812764,86.3127452494853,86.4157684578429,
86.518794300515,86.6219270672931,86.7251161587029,86.8284881520845,86.8987711466831,
87.0021658837311,87.1054071658464,87.2085271312386,87.3115816994476,87.4146049078053,
87.5176307504778,87.6207635172559,87.7239526086657,87.8273246020474,87.897607596645,
88.0010023336929,88.1042436158081,88.2073635812004,88.3104181494092,88.4134413577667,
88.5164672004388,88.6195999672169,88.7227890586266,88.8261610520081,88.8964440466068,
89.0132269961635,89.1295586830743,89.2451399878357,89.2739307161836),
 .UNSPECIFIED.);
#1752=B_SPLINE_CURVE_WITH_KNOTS('',3,(#164666,#164667,#164668,#164669,#164670,
#164671,#164672,#164673,#164674,#164675,#164676,#164677,#164678,#164679,
#164680,#164681,#164682,#164683,#164684,#164685,#164686,#164687,#164688,
#164689,#164690,#164691,#164692,#164693,#164694,#164695,#164696,#164697,
#164698,#164699,#164700,#164701,#164702,#164703,#164704,#164705,#164706,
#164707,#164708,#164709,#164710,#164711,#164712,#164713,#164714,#164715,
#164716,#164717,#164718,#164719,#164720,#164721,#164722,#164723,#164724,
#164725,#164726,#164727,#164728,#164729,#164730,#164731,#164732,#164733,
#164734,#164735,#164736,#164737,#164738,#164739,#164740,#164741,#164742,
#164743,#164744,#164745,#164746,#164747,#164748,#164749,#164750,#164751,
#164752,#164753,#164754,#164755,#164756,#164757,#164758,#164759,#164760,
#164761,#164762,#164763,#164764,#164765,#164766,#164767,#164768,#164769,
#164770,#164771,#164772,#164773,#164774,#164775,#164776,#164777,#164778,
#164779,#164780,#164781,#164782,#164783,#164784,#164785,#164786,#164787,
#164788,#164789,#164790,#164791,#164792,#164793,#164794,#164795,#164796,
#164797,#164798,#164799,#164800,#164801,#164802,#164803,#164804,#164805,
#164806,#164807,#164808,#164809,#164810,#164811,#164812,#164813,#164814,
#164815,#164816,#164817,#164818,#164819,#164820,#164821,#164822,#164823,
#164824,#164825,#164826,#164827,#164828,#164829,#164830,#164831,#164832,
#164833,#164834,#164835,#164836,#164837,#164838,#164839,#164840,#164841,
#164842,#164843,#164844,#164845,#164846,#164847,#164848,#164849,#164850,
#164851,#164852,#164853,#164854,#164855,#164856,#164857,#164858,#164859,
#164860,#164861,#164862,#164863,#164864,#164865,#164866,#164867,#164868,
#164869,#164870,#164871,#164872,#164873,#164874,#164875,#164876,#164877,
#164878,#164879,#164880,#164881,#164882,#164883),.UNSPECIFIED.,.F.,.F.,
(4,2,2,2,2,2,2,2,2,2,2,2,2,2,2,2,2,2,2,2,2,2,2,2,2,2,2,2,2,2,2,2,2,2,2,
2,2,2,2,2,2,2,2,2,2,2,2,2,2,2,2,2,2,2,2,2,2,2,2,2,2,2,2,2,2,2,2,2,2,2,2,
2,2,2,2,2,2,2,2,2,2,2,2,2,2,2,2,2,2,2,2,2,2,2,2,2,2,2,2,2,2,2,2,2,2,2,2,
2,4),(1.40868741081837,1.45282114574026,1.47138519875834,1.47413177679089,
1.47548761578519,1.47655987155254,1.4778109953015,1.48005790009866,1.49092124667973,
1.5151268521298,1.55576058997058,1.57471715275601,1.57847201680425,1.58087920003979,
1.58279727863786,1.58496151875286,1.58861884365142,1.60315479954775,1.63041096933856,
1.67885891028047,1.68487663847429,1.68679600014785,1.68797464733558,1.68906339401333,
1.69055035593317,1.69399567412729,1.72058648372916,1.74987872522115,1.78575915275887,
1.79048218761372,1.79290596228412,1.79482581833564,1.79697999747668,1.80059135438659,
1.81456962428922,1.86539442246418,1.89525060834919,1.89816654566859,1.89955590972665,
1.90063131619709,1.9018598981651,1.9040035678585,1.91330194616448,1.93215135579698,
1.97256231653036,1.98482739612756,1.99945074480414,2.0032415632813,2.00545767029186,
2.0073706717409,2.00970632810299,2.01415658502488,2.04502863803953,2.09142711888106,
2.10771915549577,2.11035260598368,2.11170331311897,2.11277538648445,2.11403077664091,
2.11629662263216,2.12747402129667,2.15286648941136,2.20673784874064,2.21356422178613,
2.21642053034251,2.2182122676365,2.22017665378882,2.22289578986132,2.22938634569801,
2.25856105646812,2.30111524236714,2.31970024688058,2.32244781926679,2.32380398246119,
2.32487641294606,2.32612764658098,2.3283745138691,2.33923315584635,2.36341874369873,
2.41908468850141,2.42574444335819,2.42828998172059,2.43011817371655,2.4320183137549,
2.43450383031192,2.43725314588343,2.44183093288911,2.45123417697265,2.47774179575797,
2.51518035463293,2.51690561967688,2.52220690407069,2.53248598616245,2.53458334527713,
2.53592493386245,2.53699633411449,2.53825858113818,2.54055637530816,2.55230118277678,
2.60144042319159,2.62013544234763,2.63560978979366,2.63947549573205,2.64170872938115,
2.64343985595649,2.64525080325019,2.64744527432452,2.6506882096222,2.66858622124742),
 .UNSPECIFIED.);
#1753=B_SPLINE_CURVE_WITH_KNOTS('',3,(#164884,#164885,#164886,#164887,#164888,
#164889,#164890,#164891,#164892,#164893),.UNSPECIFIED.,.F.,.F.,(4,3,3,4),
(-85.8723819833138,-85.7556990490293,-85.639073538087,-85.5224480271446),
 .UNSPECIFIED.);
#1754=B_SPLINE_CURVE_WITH_KNOTS('',3,(#164898,#164899,#164900,#164901,#164902,
#164903,#164904,#164905,#164906,#164907,#164908,#164909,#164910,#164911,
#164912,#164913,#164914,#164915,#164916,#164917,#164918,#164919,#164920,
#164921,#164922,#164923,#164924,#164925,#164926,#164927,#164928,#164929,
#164930,#164931,#164932,#164933,#164934,#164935,#164936,#164937,#164938,
#164939,#164940,#164941,#164942,#164943,#164944,#164945,#164946,#164947,
#164948,#164949,#164950,#164951,#164952,#164953,#164954,#164955,#164956,
#164957,#164958,#164959,#164960,#164961,#164962,#164963,#164964,#164965,
#164966,#164967,#164968,#164969,#164970,#164971,#164972,#164973,#164974,
#164975,#164976,#164977,#164978,#164979,#164980,#164981,#164982,#164983,
#164984,#164985,#164986,#164987,#164988,#164989,#164990,#164991,#164992,
#164993,#164994,#164995,#164996,#164997,#164998,#164999,#165000,#165001,
#165002,#165003,#165004,#165005,#165006,#165007,#165008,#165009,#165010,
#165011,#165012,#165013,#165014,#165015,#165016,#165017,#165018,#165019,
#165020,#165021,#165022,#165023,#165024,#165025,#165026,#165027,#165028,
#165029,#165030,#165031,#165032,#165033,#165034,#165035,#165036,#165037,
#165038,#165039,#165040,#165041,#165042,#165043,#165044,#165045,#165046,
#165047,#165048,#165049,#165050,#165051,#165052,#165053,#165054,#165055,
#165056,#165057,#165058,#165059,#165060,#165061,#165062,#165063,#165064,
#165065,#165066,#165067,#165068,#165069,#165070,#165071,#165072,#165073,
#165074,#165075,#165076,#165077,#165078,#165079,#165080,#165081,#165082,
#165083,#165084,#165085,#165086,#165087,#165088,#165089,#165090,#165091,
#165092,#165093,#165094,#165095,#165096,#165097,#165098,#165099,#165100,
#165101,#165102,#165103,#165104,#165105,#165106,#165107,#165108,#165109,
#165110,#165111,#165112,#165113,#165114,#165115,#165116,#165117,#165118,
#165119,#165120,#165121,#165122,#165123,#165124,#165125,#165126,#165127,
#165128,#165129),.UNSPECIFIED.,.F.,.F.,(4,2,2,2,2,2,2,2,2,2,2,2,2,2,2,2,
2,2,2,2,2,2,2,2,2,2,2,2,2,2,2,2,2,2,2,2,2,2,2,2,2,2,2,2,2,2,2,2,2,2,2,2,
2,2,2,2,2,2,2,2,2,2,2,2,2,2,2,2,2,2,2,2,2,2,2,2,2,2,2,2,2,2,2,2,2,2,2,2,
2,2,2,2,2,2,2,2,2,2,2,2,2,2,2,2,2,2,2,2,2,2,2,2,2,2,2,4),(1.26002615597782,
1.26028070805043,1.26243765844669,1.26366897184768,1.26474360947128,1.26612781377373,
1.26901832820632,1.29472133876866,1.33416803952351,1.36189145497452,1.36603205869553,
1.36852853416931,1.37046258464448,1.37255606241967,1.37589461278971,1.38701080285806,
1.40539635323422,1.4527492291279,1.47131192493545,1.47405830345727,1.47541404406432,
1.47648622207153,1.47773725514394,1.47998399723173,1.4908465597794,1.51505042368327,
1.55568120554435,1.57463638800517,1.57839097932564,1.58079798786816,1.58271592736377,
1.58488001062529,1.58853707070335,1.60307197732221,1.63032618449044,1.67877073002063,
1.68478791337691,1.68670712240226,1.68788568111764,1.68897435003655,1.69046121140794,
1.69390632131056,1.72150369537025,1.75670359743434,1.78588842039213,1.79006778318002,
1.79257577918699,1.79451177788885,1.79660044572339,1.79991645399402,1.81082150801718,
1.82871959207018,1.87939916826945,1.89553735609574,1.89816679294372,1.89951654559467,
1.90058843991112,1.90184428978855,1.90411265949309,1.91533666153275,1.94091152279756,
1.99450684191176,2.00135460355215,2.00421424001118,2.00600643001736,2.00796999337776,
2.01068556187289,2.01715599963737,2.07136894588758,2.10734801499149,2.11021314503983,
2.11159256056708,2.11266692187228,2.11390180578823,2.11607423748684,2.12578094808153,
2.17476207518025,2.20992245583459,2.21421041223912,2.21675010787067,2.21869121070358,
2.22076649111642,2.2240214160925,2.23437878726975,2.25104272870629,2.28402275387341,
2.30302734564579,2.30404951385746,2.31976336255357,2.32237134124086,2.32371643803482,
2.32478799036656,2.3260473364914,2.32833195266626,2.33984138667691,2.36654348994477,
2.41852437352912,2.42549083804804,2.42836994827758,2.43016562485505,2.43208673814767,
2.43469532868378,2.43761573579464,2.44261318292921,2.4532382945637,2.48450054508195,
2.52882031075396,2.53348992219872,2.53522377222595,2.5362481016298,2.53734184502224,
2.53885840904915,2.54247568196251,2.54756136826203,2.56162299028348,2.59401617871736),
 .UNSPECIFIED.);
#1755=B_SPLINE_CURVE_WITH_KNOTS('',3,(#165131,#165132,#165133,#165134,#165135,
#165136,#165137,#165138,#165139,#165140,#165141,#165142,#165143,#165144,
#165145,#165146,#165147,#165148,#165149,#165150,#165151,#165152,#165153,
#165154,#165155,#165156,#165157,#165158,#165159,#165160,#165161,#165162,
#165163,#165164,#165165,#165166,#165167,#165168,#165169,#165170,#165171,
#165172,#165173,#165174,#165175,#165176,#165177,#165178,#165179,#165180,
#165181,#165182,#165183,#165184,#165185,#165186,#165187,#165188,#165189,
#165190,#165191,#165192,#165193,#165194,#165195,#165196,#165197,#165198,
#165199,#165200,#165201,#165202,#165203,#165204,#165205,#165206,#165207,
#165208,#165209,#165210,#165211,#165212,#165213,#165214,#165215,#165216,
#165217,#165218,#165219,#165220,#165221,#165222,#165223,#165224,#165225,
#165226,#165227,#165228,#165229,#165230,#165231,#165232,#165233,#165234,
#165235,#165236,#165237,#165238,#165239,#165240,#165241,#165242,#165243,
#165244,#165245,#165246,#165247,#165248,#165249,#165250,#165251,#165252,
#165253,#165254,#165255,#165256,#165257,#165258,#165259,#165260,#165261,
#165262,#165263,#165264,#165265,#165266,#165267,#165268,#165269,#165270,
#165271,#165272,#165273,#165274,#165275,#165276,#165277,#165278,#165279,
#165280,#165281,#165282,#165283,#165284,#165285,#165286,#165287,#165288,
#165289,#165290,#165291,#165292,#165293,#165294,#165295,#165296,#165297,
#165298,#165299,#165300,#165301,#165302,#165303,#165304,#165305,#165306,
#165307,#165308,#165309,#165310,#165311),.UNSPECIFIED.,.F.,.F.,(4,3,3,3,
3,3,3,3,3,3,3,3,3,3,3,3,3,3,3,3,3,3,3,3,3,3,3,3,3,3,3,3,3,3,3,3,3,3,3,3,
3,3,3,3,3,3,3,3,3,3,3,3,3,3,3,3,3,3,3,3,4),(-91.8056330559184,-91.703478392043,
-91.6014794906832,-91.4995669524773,-91.3977052133679,-91.2958587787063,
-91.1939207704849,-91.0919397623249,-90.989771706694,-90.8941169465306,
-90.7907222094828,-90.6874809273678,-90.5843609619755,-90.4813063937666,
-90.378283185409,-90.2752573427367,-90.1721245759587,-90.068935484549,-89.9655634911674,
-89.8952804965687,-89.7918857595207,-89.6886444774058,-89.5855245120134,
-89.4824699438044,-89.3794467354466,-89.2764208927741,-89.173288125996,
-89.0700990345862,-88.9667270412044,-88.8964440466068,-88.793049309559,
-88.6898080274439,-88.5866880620516,-88.4836334938427,-88.3806102854849,
-88.2775844428122,-88.1744516760342,-88.0712625846245,-87.9678905912428,
-87.897607596645,-87.794212859597,-87.690971577482,-87.5878516120898,-87.4847970438808,
-87.3817738355229,-87.2787479928504,-87.1756152260723,-87.0724261346625,
-86.9690541412809,-86.8987711466831,-86.7953764096353,-86.69213512752,-86.5890151621277,
-86.4859605939189,-86.382937385561,-86.279911542888,-86.1767787761099,-86.0735896847,
-85.9702176913185,-85.8999346967212,-85.8723819833138),.UNSPECIFIED.);
#1756=B_SPLINE_CURVE_WITH_KNOTS('',3,(#165312,#165313,#165314,#165315,#165316),
 .UNSPECIFIED.,.F.,.F.,(4,1,4),(-92.1566392527806,-91.8929533964925,-91.8056333339369),
 .UNSPECIFIED.);
#1757=B_SPLINE_CURVE_WITH_KNOTS('',3,(#165322,#165323,#165324,#165325,#165326,
#165327,#165328,#165329,#165330,#165331,#165332,#165333,#165334,#165335,
#165336,#165337,#165338,#165339,#165340,#165341),.UNSPECIFIED.,.F.,.F.,
(4,2,2,2,2,2,2,2,2,4),(2.59390681890108,2.64803077420865,2.65590234473983,
2.65799832092765,2.65922828409126,2.66028508238674,2.66133096658783,2.66268138243313,
2.66513940918834,2.66823303858644),.UNSPECIFIED.);
#1758=B_SPLINE_CURVE_WITH_KNOTS('',3,(#165342,#165343,#165344,#165345,#165346,
#165347,#165348,#165349,#165350,#165351,#165352,#165353,#165354,#165355,
#165356,#165357,#165358,#165359,#165360,#165361,#165362,#165363,#165364,
#165365,#165366,#165367,#165368,#165369,#165370,#165371,#165372,#165373,
#165374,#165375,#165376,#165377,#165378,#165379,#165380,#165381,#165382,
#165383,#165384,#165385,#165386,#165387,#165388,#165389,#165390,#165391,
#165392,#165393,#165394,#165395,#165396,#165397,#165398,#165399,#165400,
#165401,#165402,#165403,#165404,#165405,#165406,#165407,#165408,#165409,
#165410,#165411,#165412,#165413,#165414,#165415,#165416,#165417,#165418,
#165419,#165420,#165421,#165422,#165423,#165424,#165425,#165426,#165427,
#165428,#165429,#165430,#165431,#165432,#165433,#165434,#165435,#165436,
#165437,#165438,#165439,#165440,#165441,#165442,#165443,#165444,#165445,
#165446,#165447,#165448,#165449,#165450,#165451,#165452,#165453,#165454,
#165455,#165456,#165457,#165458,#165459,#165460,#165461,#165462,#165463,
#165464,#165465,#165466,#165467,#165468,#165469,#165470,#165471,#165472,
#165473,#165474,#165475,#165476,#165477,#165478,#165479,#165480,#165481,
#165482,#165483,#165484,#165485,#165486,#165487,#165488,#165489,#165490,
#165491,#165492,#165493,#165494,#165495,#165496,#165497,#165498,#165499,
#165500,#165501,#165502,#165503,#165504,#165505,#165506,#165507,#165508,
#165509,#165510,#165511,#165512,#165513,#165514,#165515,#165516,#165517,
#165518,#165519,#165520,#165521,#165522,#165523,#165524,#165525,#165526,
#165527,#165528,#165529,#165530,#165531,#165532,#165533,#165534,#165535,
#165536,#165537,#165538,#165539,#165540,#165541,#165542,#165543,#165544,
#165545,#165546,#165547,#165548,#165549,#165550,#165551,#165552,#165553,
#165554,#165555,#165556,#165557,#165558,#165559,#165560,#165561,#165562,
#165563,#165564,#165565,#165566,#165567,#165568,#165569,#165570,#165571,
#165572,#165573,#165574,#165575,#165576,#165577,#165578,#165579,#165580,
#165581,#165582,#165583),.UNSPECIFIED.,.F.,.F.,(4,2,2,2,2,2,2,2,2,2,2,2,
2,2,2,2,2,2,2,2,2,2,2,2,2,2,2,2,2,2,2,2,2,2,2,2,2,2,2,2,2,2,2,2,2,2,2,2,
2,2,2,2,2,2,2,2,2,2,2,2,2,2,2,2,2,2,2,2,2,2,2,2,2,2,2,2,2,2,2,2,2,2,2,2,
2,2,2,2,2,2,2,2,2,2,2,2,2,2,2,2,2,2,2,2,2,2,2,2,2,2,2,2,2,2,2,2,2,2,2,2,
4),(0.000817339072717396,0.0612254327528195,0.0876737705967202,0.0938318736697624,
0.0964929805366432,0.0984458542304952,0.100248359885734,0.103168886035034,
0.110389678966243,0.154249311684379,0.195394740453527,0.199213035784798,
0.201237851957825,0.202549372202172,0.203772999109811,0.203776565900573,
0.203780144963764,0.203783736777643,0.203787574314428,0.203791473684978,
0.203795436057235,0.203799463015975,0.203803555948668,0.203807715984486,
0.203811944716874,0.203816243954876,0.203820615083323,0.203825059546327,
0.203829579099047,0.203834175258828,0.203838849929433,0.203843605092771,
0.203848442246181,0.204892136000352,0.206274788297811,0.20915947304974,
0.243327703493716,0.277568497356708,0.294122448124397,0.304429297822026,
0.307677059612904,0.309749872128427,0.311690141237809,0.31423087396419,
0.318525380427928,0.353659954588658,0.402633763010693,0.412337348700009,
0.414508647350004,0.415742808062672,0.416816494385944,0.418194973612607,
0.421057933634848,0.45665134743274,0.489504290229703,0.506061808151536,
0.516370537069155,0.519618709137008,0.521691739801433,0.52363218241276,
0.526173098043653,0.530467814386623,0.565590939106778,0.614523621310496,
0.624282119736505,0.626457330666071,0.627692422823497,0.628766091559657,
0.630143465734079,0.633000400899712,0.656099199057216,0.698304056580163,
0.716918313426454,0.728132929179101,0.731481262618382,0.73357646712124,
0.735509119134418,0.737999605418669,0.742121252942593,0.769138869453326,
0.823719433370545,0.836002065275706,0.838327871257832,0.83959584527571,
0.840666381763847,0.84199968538415,0.84407103513996,0.853972468995163,0.859516307815003,
0.859961922570091,0.866849346951346,0.880575423486423,0.913435731176484,
0.929997286362807,0.94030843369783,0.943557317130617,0.945630789628183,
0.94757163726462,0.950113070921443,0.954408635198058,0.989535041580374,
1.03846544714543,1.04824086681503,1.05041755166975,1.0516531268085,1.05272698887713,
1.05410431501674,1.05696013201451,1.07974137623904,1.092585151773,1.12544038801377,
1.14199337745437,1.15230094909718,1.15554964135732,1.15762321668979,1.15956431854414,
1.1621063130231,1.16640333617586,1.20161017838112,1.25079154582779,1.26002615597782),
 .UNSPECIFIED.);
#1759=B_SPLINE_CURVE_WITH_KNOTS('',3,(#165585,#165586,#165587,#165588,#165589,
#165590,#165591,#165592,#165593,#165594),.UNSPECIFIED.,.F.,.F.,(4,1,1,1,
1,1,1,4),(-98.0888186411165,-97.8859720962637,-96.8871356463018,-95.88829919634,
-94.8894627463781,-93.8906262964162,-92.8917898464543,-92.1566392527806),
 .UNSPECIFIED.);
#1760=B_SPLINE_CURVE_WITH_KNOTS('',3,(#165595,#165596,#165597,#165598,#165599,
#165600,#165601,#165602,#165603,#165604,#165605,#165606,#165607,#165608,
#165609,#165610,#165611,#165612,#165613,#165614),.UNSPECIFIED.,.F.,.F.,
(4,2,2,2,2,2,2,2,2,4),(0.000629226362741632,0.0468682715409837,0.0541782011601138,
0.0579984688717706,0.0612790161803505,0.0633591116006488,0.065296700611161,
0.0678203279030634,0.0720557143177805,0.0751037492301708),.UNSPECIFIED.);
#1761=B_SPLINE_CURVE_WITH_KNOTS('',3,(#165619,#165620,#165621,#165622,#165623,
#165624,#165625,#165626,#165627,#165628,#165629,#165630,#165631,#165632,
#165633,#165634,#165635,#165636,#165637,#165638,#165639,#165640,#165641,
#165642,#165643,#165644,#165645,#165646,#165647,#165648,#165649,#165650,
#165651,#165652,#165653,#165654,#165655,#165656,#165657,#165658,#165659,
#165660,#165661,#165662,#165663,#165664,#165665,#165666,#165667,#165668,
#165669,#165670,#165671,#165672,#165673,#165674,#165675,#165676,#165677,
#165678,#165679,#165680,#165681,#165682,#165683,#165684,#165685,#165686,
#165687,#165688,#165689,#165690,#165691,#165692,#165693,#165694,#165695,
#165696,#165697,#165698,#165699,#165700,#165701,#165702,#165703,#165704,
#165705,#165706,#165707,#165708,#165709,#165710,#165711,#165712,#165713,
#165714,#165715,#165716,#165717,#165718,#165719,#165720,#165721,#165722,
#165723,#165724,#165725,#165726,#165727,#165728,#165729,#165730,#165731,
#165732,#165733,#165734,#165735,#165736,#165737,#165738,#165739,#165740,
#165741,#165742,#165743,#165744,#165745,#165746,#165747,#165748,#165749,
#165750,#165751,#165752,#165753,#165754,#165755,#165756,#165757,#165758,
#165759,#165760,#165761,#165762,#165763,#165764,#165765,#165766,#165767,
#165768,#165769,#165770,#165771,#165772,#165773,#165774,#165775,#165776,
#165777,#165778,#165779,#165780,#165781,#165782,#165783,#165784,#165785,
#165786,#165787,#165788,#165789,#165790,#165791,#165792,#165793,#165794,
#165795,#165796,#165797,#165798,#165799,#165800,#165801,#165802,#165803,
#165804,#165805,#165806,#165807,#165808,#165809,#165810,#165811,#165812,
#165813,#165814,#165815,#165816,#165817,#165818,#165819,#165820,#165821,
#165822,#165823,#165824,#165825,#165826,#165827,#165828,#165829,#165830,
#165831,#165832,#165833,#165834,#165835,#165836,#165837,#165838,#165839,
#165840,#165841,#165842,#165843,#165844,#165845,#165846,#165847,#165848,
#165849,#165850,#165851,#165852,#165853,#165854,#165855,#165856,#165857,
#165858),.UNSPECIFIED.,.F.,.F.,(4,2,2,2,2,2,2,2,2,2,2,2,2,2,2,2,2,2,2,2,
2,2,2,2,2,2,2,2,2,2,2,2,2,2,2,2,2,2,2,2,2,2,2,2,2,2,2,2,2,2,2,2,2,2,2,2,
2,2,2,2,2,2,2,2,2,2,2,2,2,2,2,2,2,2,2,2,2,2,2,2,2,2,2,2,2,2,2,2,2,2,2,2,
2,2,2,2,2,2,2,2,2,2,2,2,2,2,2,2,2,2,2,2,2,2,2,2,2,2,2,4),(1.26010921737026,
1.26507519904627,1.27555923729397,1.27882825410422,1.28090642691018,1.28284598073427,
1.28537754430456,1.289638197626,1.3346351541466,1.37968330383748,1.3844082086735,
1.3861503997765,1.38717632884007,1.38826895714846,1.38977937103468,1.39336075837539,
1.43099589455533,1.48141556130892,1.48847363970178,1.49136787137908,1.49316625195796,
1.49512425137757,1.49780965364733,1.50410317390092,1.53164024864648,1.56004209019016,
1.58237053593612,1.5950765993546,1.59731700586766,1.59870195523859,1.59977669542454,
1.60100760130327,1.60316258464822,1.61262356863888,1.66180558128258,1.69700796564163,
1.70130493692629,1.70384701200501,1.70578822854744,1.70786197700883,1.71111104496496,
1.72142060427254,1.73797984807966,1.77086947219409,1.78460338246217,1.79147582093191,
1.79169109545741,1.79518015772773,1.80716705030004,1.8093685823388,1.81074174855965,
1.81181528521042,1.81305379946272,1.81524362016794,1.82521222274992,1.87395926435719,
1.90902084475786,1.91331569651985,1.91585706580136,1.91779805907657,1.91987187516282,
1.92312168834769,1.93343900250753,1.95001583226262,1.98291872545002,1.99803667495543,
2.00292469361331,2.01883478782531,2.02144944463696,2.02279578282252,2.02386716213014,
2.02512495642997,2.02740331687887,2.03880954001362,2.06510468833873,2.1176375520257,
2.12456375774258,2.12743578826596,2.12922985062767,2.13119073204009,2.13389391795494,
2.14029379588092,2.18941824182025,2.22775583662013,2.23251803597426,2.23426570143994,
2.23529257860472,2.23638429695794,2.23789033096065,2.24144708894313,2.27664190372315,
2.3297665595455,2.33664873732664,2.33951356055126,2.34130633905714,2.3432684043734,
2.3459779654706,2.35241537963936,2.38115170514505,2.4253317692948,2.42894637740709,
2.44306264667357,2.44537282296395,2.44676354558292,2.44780989200213,2.4489851033896,
2.45023044687475,2.45209499031907,2.45549251038601,2.46337194216412,2.51337437630157,
2.54520995529924,2.5494477005681,2.55197237865418,2.55391055729918,2.55599107212067,
2.55927182787169,2.5698633194134,2.58705194835977,2.59390681890108),
 .UNSPECIFIED.);
#1762=B_SPLINE_CURVE_WITH_KNOTS('',3,(#165859,#165860,#165861,#165862,#165863,
#165864,#165865,#165866,#165867,#165868,#165869,#165870,#165871,#165872,
#165873,#165874,#165875,#165876,#165877,#165878,#165879,#165880,#165881,
#165882,#165883,#165884,#165885,#165886,#165887,#165888,#165889,#165890,
#165891,#165892,#165893,#165894,#165895,#165896,#165897,#165898,#165899,
#165900,#165901,#165902,#165903,#165904,#165905,#165906,#165907,#165908,
#165909,#165910,#165911,#165912,#165913,#165914,#165915,#165916,#165917,
#165918,#165919,#165920,#165921,#165922,#165923,#165924,#165925,#165926,
#165927,#165928,#165929,#165930,#165931,#165932,#165933,#165934,#165935,
#165936,#165937,#165938,#165939,#165940,#165941,#165942,#165943,#165944,
#165945,#165946,#165947,#165948,#165949,#165950,#165951,#165952,#165953,
#165954,#165955,#165956,#165957,#165958,#165959,#165960,#165961,#165962,
#165963,#165964,#165965,#165966,#165967,#165968,#165969,#165970,#165971,
#165972,#165973,#165974,#165975,#165976,#165977,#165978,#165979,#165980,
#165981,#165982,#165983,#165984,#165985,#165986,#165987,#165988,#165989,
#165990,#165991,#165992,#165993,#165994,#165995,#165996,#165997,#165998,
#165999,#166000,#166001,#166002,#166003,#166004,#166005,#166006,#166007,
#166008,#166009,#166010,#166011,#166012,#166013,#166014,#166015,#166016,
#166017,#166018,#166019,#166020,#166021,#166022,#166023,#166024,#166025,
#166026,#166027,#166028,#166029,#166030,#166031,#166032,#166033,#166034,
#166035,#166036,#166037,#166038,#166039,#166040,#166041,#166042,#166043,
#166044,#166045,#166046,#166047,#166048,#166049,#166050,#166051,#166052,
#166053,#166054,#166055,#166056,#166057,#166058,#166059,#166060,#166061,
#166062,#166063,#166064,#166065,#166066,#166067,#166068,#166069,#166070,
#166071,#166072,#166073,#166074,#166075,#166076,#166077,#166078),
 .UNSPECIFIED.,.F.,.F.,(4,2,2,2,2,2,2,2,2,2,2,2,2,2,2,2,2,2,2,2,2,2,2,2,
2,2,2,2,2,2,2,2,2,2,2,2,2,2,2,2,2,2,2,2,2,2,2,2,2,2,2,2,2,2,2,2,2,2,2,2,
2,2,2,2,2,2,2,2,2,2,2,2,2,2,2,2,2,2,2,2,2,2,2,2,2,2,2,2,2,2,2,2,2,2,2,2,
2,2,2,2,2,2,2,2,2,2,2,2,2,4),(0.0751037492301708,0.118880917795946,0.139376817903217,
0.162219030290009,0.1668645224268,0.168156402197407,0.169384240099947,0.170458911131563,
0.171847203283008,0.174760478527842,0.204939955840196,0.25644351367738,
0.26944615321281,0.272989263665715,0.275127428116121,0.27704870403762,0.279495695920477,
0.283383389282271,0.304699992500162,0.352239606498166,0.369333915622309,
0.37805575371251,0.380155277212108,0.381373589679308,0.382450006624803,
0.383830705743057,0.38610757303591,0.39954906470426,0.401671935001865,0.405953171131185,
0.448938066353763,0.476874669080311,0.483215758041737,0.485908528233608,
0.487867146392035,0.489662804304886,0.492545408287964,0.499538379224643,
0.551069004424207,0.578089566859801,0.589674817009573,0.591962866590075,
0.593222562354446,0.594293485817936,0.595636612522682,0.598237329464448,
0.613805583386551,0.620261087972416,0.661675792697354,0.688947702140474,
0.695208005898256,0.697887019092948,0.699843253114721,0.701642031816917,
0.704541356783058,0.711634308872206,0.761292293849531,0.799603994996305,
0.803208308632069,0.804722262352918,0.805815169155305,0.806839547130502,
0.808575244902419,0.813260103061409,0.854341746075041,0.900771483197287,
0.907163364146536,0.909864877039203,0.911825169225872,0.913619127096042,
0.916491927392863,0.923424811140936,0.975871376244757,1.00224511615172,
1.01366959274197,1.01594870965649,1.01720652167612,1.01827767754899,1.01962342569414,
1.0222360319686,1.03808734827923,1.04283130672364,1.05810918948618,1.09098449621427,
1.1075660460329,1.1178860027798,1.12113572695467,1.12320927143933,1.12514986022135,
1.12769048434938,1.13198362594672,1.17438369867638,1.20344098471063,1.22305680282963,
1.22701196143879,1.2285836225058,1.22968719560523,1.23069765501811,1.2323612612938,
1.23658634211238,1.28592939951302,1.32669781224683,1.33176406047032,1.33422368661709,
1.33614666424004,1.33827828718448,1.34179101576568,1.35466697760074,1.37736927597896,
1.40852037702754),.UNSPECIFIED.);
#1763=B_SPLINE_CURVE_WITH_KNOTS('',3,(#166084,#166085,#166086,#166087),
 .UNSPECIFIED.,.F.,.F.,(4,4),(114.406674973252,114.756144714286),
 .UNSPECIFIED.);
#1764=B_SPLINE_CURVE_WITH_KNOTS('',3,(#166088,#166089,#166090,#166091,#166092,
#166093,#166094,#166095,#166096,#166097,#166098,#166099,#166100,#166101,
#166102,#166103,#166104,#166105,#166106,#166107,#166108,#166109,#166110,
#166111,#166112,#166113,#166114,#166115,#166116,#166117,#166118,#166119,
#166120,#166121,#166122,#166123,#166124,#166125,#166126,#166127,#166128,
#166129,#166130,#166131,#166132,#166133,#166134,#166135,#166136,#166137,
#166138,#166139,#166140,#166141,#166142,#166143,#166144,#166145,#166146,
#166147,#166148,#166149,#166150,#166151,#166152,#166153,#166154,#166155,
#166156,#166157,#166158,#166159,#166160,#166161,#166162,#166163,#166164,
#166165,#166166,#166167,#166168,#166169,#166170,#166171,#166172,#166173,
#166174,#166175,#166176,#166177,#166178,#166179,#166180,#166181,#166182,
#166183,#166184,#166185,#166186,#166187,#166188,#166189,#166190,#166191,
#166192,#166193,#166194,#166195,#166196,#166197,#166198,#166199,#166200,
#166201,#166202,#166203,#166204,#166205,#166206,#166207,#166208,#166209,
#166210,#166211,#166212,#166213,#166214,#166215,#166216,#166217,#166218,
#166219,#166220,#166221,#166222,#166223,#166224,#166225,#166226,#166227,
#166228,#166229,#166230,#166231,#166232,#166233,#166234,#166235,#166236,
#166237,#166238,#166239,#166240,#166241,#166242,#166243,#166244,#166245,
#166246,#166247,#166248,#166249,#166250,#166251,#166252,#166253,#166254,
#166255,#166256,#166257,#166258,#166259,#166260,#166261,#166262,#166263,
#166264,#166265,#166266,#166267,#166268,#166269,#166270,#166271,#166272,
#166273,#166274,#166275,#166276,#166277,#166278,#166279,#166280,#166281,
#166282,#166283,#166284,#166285,#166286,#166287,#166288,#166289,#166290,
#166291,#166292,#166293,#166294,#166295,#166296,#166297,#166298,#166299,
#166300,#166301,#166302,#166303,#166304,#166305),.UNSPECIFIED.,.F.,.F.,
(4,2,2,2,2,2,2,2,2,2,2,2,2,2,2,2,2,2,2,2,2,2,2,2,2,2,2,2,2,2,2,2,2,2,2,
2,2,2,2,2,2,2,2,2,2,2,2,2,2,2,2,2,2,2,2,2,2,2,2,2,2,2,2,2,2,2,2,2,2,2,2,
2,2,2,2,2,2,2,2,2,2,2,2,2,2,2,2,2,2,2,2,2,2,2,2,2,2,2,2,2,2,2,2,2,2,2,2,
2,4),(0.000658789515707303,0.00332970180415904,0.00592165902641297,0.00778879700177709,
0.00964368955138184,0.0114909186089904,0.0146445375462132,0.0233614963763356,
0.0882031581702577,0.10859694712227,0.112633279300404,0.114217804455085,
0.115323920171485,0.116331747666332,0.117981260296211,0.122122285944367,
0.172468751005332,0.209103911759757,0.21404883968213,0.216947679594109,
0.219546315887063,0.221463438656713,0.223262615789461,0.226163322652698,
0.233240925903314,0.283134745524853,0.321237734036367,0.32484039700091,
0.326354173578048,0.32744714437323,0.328471734809312,0.330208116667581,
0.334896706617737,0.375891352156246,0.422413598326696,0.428806451658905,
0.431508314614591,0.433468838592159,0.435262993252094,0.438136075204148,
0.445069465778075,0.497521833869186,0.523899061692082,0.535324964039552,
0.537604348547007,0.538862306004373,0.539933584374217,0.541279484692083,
0.543892381332811,0.559745117646786,0.564467327213708,0.609730512029555,
0.628225324282423,0.639389069357717,0.642732263372665,0.644826500865052,
0.646759789689279,0.649253234594747,0.653384405443102,0.68075952231016,
0.723082618470413,0.739259590348515,0.7476688771705,0.749744014098205,0.750957103079242,
0.752034946544863,0.753425291596481,0.755734300121712,0.769827652572318,
0.772669413539149,0.822247298681764,0.840396918145557,0.851411582559185,
0.854738789655328,0.856829496553685,0.858763954196761,0.861265124926505,
0.865422615588646,0.893801367847194,0.947093326898015,0.959257576785838,
0.961577403978429,0.962844177535305,0.963914919843751,0.965250013507755,
0.967326916370838,0.97730575193491,0.98291454772312,0.992312010149648,1.00388099133634,
1.03672569067058,1.05326574937608,1.06356749723049,1.06681554095262,1.06888898776942,
1.07083016989094,1.07337255897637,1.07767089828658,1.11297880245535,1.16222997987263,
1.17156701784788,1.17371313167014,1.17494206414828,1.17601709842688,1.17740507541625,
1.18031492369544,1.20844434728681,1.24813083709657,1.26010921737026),
 .UNSPECIFIED.);
#1765=B_SPLINE_CURVE_WITH_KNOTS('',3,(#166307,#166308,#166309,#166310,#166311,
#166312,#166313,#166314,#166315,#166316,#166317,#166318,#166319,#166320,
#166321,#166322,#166323,#166324,#166325,#166326,#166327,#166328,#166329,
#166330,#166331,#166332,#166333,#166334,#166335,#166336,#166337,#166338,
#166339,#166340,#166341,#166342,#166343,#166344,#166345,#166346,#166347,
#166348,#166349,#166350,#166351,#166352,#166353,#166354,#166355,#166356,
#166357,#166358,#166359,#166360,#166361,#166362,#166363,#166364,#166365,
#166366,#166367,#166368,#166369,#166370,#166371,#166372,#166373,#166374,
#166375,#166376,#166377,#166378,#166379,#166380,#166381,#166382,#166383,
#166384,#166385,#166386,#166387,#166388,#166389,#166390,#166391,#166392,
#166393,#166394,#166395,#166396,#166397,#166398,#166399,#166400,#166401,
#166402,#166403,#166404,#166405,#166406,#166407,#166408,#166409,#166410,
#166411,#166412,#166413,#166414,#166415,#166416,#166417,#166418,#166419,
#166420,#166421,#166422,#166423,#166424,#166425,#166426,#166427,#166428,
#166429,#166430,#166431,#166432,#166433,#166434,#166435,#166436,#166437,
#166438,#166439,#166440,#166441,#166442,#166443,#166444,#166445,#166446,
#166447,#166448,#166449,#166450,#166451,#166452,#166453,#166454,#166455,
#166456,#166457,#166458,#166459,#166460,#166461,#166462,#166463,#166464,
#166465,#166466,#166467,#166468,#166469,#166470,#166471,#166472,#166473,
#166474,#166475,#166476,#166477,#166478,#166479,#166480,#166481,#166482,
#166483,#166484,#166485,#166486,#166487,#166488,#166489,#166490,#166491,
#166492,#166493,#166494,#166495,#166496,#166497,#166498,#166499,#166500,
#166501,#166502,#166503,#166504,#166505,#166506,#166507,#166508,#166509,
#166510,#166511,#166512,#166513,#166514,#166515,#166516,#166517,#166518,
#166519,#166520,#166521,#166522,#166523,#166524,#166525,#166526),
 .UNSPECIFIED.,.F.,.F.,(4,2,2,2,2,2,2,2,2,2,2,2,2,2,2,2,2,2,2,2,2,2,2,2,
2,2,2,2,2,2,2,2,2,2,2,2,2,2,2,2,2,2,2,2,2,2,2,2,2,2,2,2,2,2,2,2,2,2,2,2,
2,2,2,2,2,2,2,2,2,2,2,2,2,2,2,2,2,2,2,2,2,2,2,2,2,2,2,2,2,2,2,2,2,2,2,2,
2,2,2,2,2,2,2,2,2,2,2,2,2,4),(1.40852037702754,1.41595952831496,1.42095388239778,
1.43696095698081,1.43958032952729,1.44092752275851,1.44199875462644,1.44325541612354,
1.44552928276432,1.45686267755102,1.48287403764511,1.53579379382189,1.5426892009883,
1.54555580767838,1.54734862205882,1.54930985839816,1.55201668258124,1.5584400525967,
1.587064212374,1.63834665401397,1.64940840938901,1.65155540412573,1.65291182923959,
1.65398373286765,1.65523350795285,1.65747565037909,1.66827109295293,1.69223143156492,
1.74818522847414,1.75481065816892,1.75734997113946,1.7591758670615,1.76111445160845,
1.76368758723061,1.76935215543428,1.79199535293755,1.82481339615918,1.82925953898682,
1.86052855248765,1.8634404249806,1.86482848821479,1.865903180561,1.8671312741363,
1.86927485860266,1.87858471365108,1.92772623338111,1.96309845209544,1.96739599507743,
1.9699377230736,1.97187828008559,1.97395094166477,1.97719750884374,1.98749241484776,
2.00402173851242,2.03687891921335,2.04844679064327,2.05789193589881,2.07294229793109,
2.07529362352922,2.07669617215181,2.0777753926561,2.07898105911017,2.08102370323427,
2.0890449570702,2.10412364450517,2.14357820280149,2.17511544237045,2.17934612522303,
2.18186837571774,2.18380572726972,2.18588637031083,2.18916947880309,2.19978736861725,
2.21703729298442,2.25266391193605,2.28437456570608,2.28728570742664,2.28867356480054,
2.28974816337607,2.29097622319617,2.29311992072815,2.30243292720451,2.3515827274682,
2.38693606851853,2.39123308462749,2.39377455913906,2.39571495608015,2.39778747911725,
2.40103389694969,2.41112434453458,2.42729141912476,2.46900282389672,2.49632888141909,
2.49923242750349,2.50061878657169,2.50169320466273,2.50292215527821,2.50421560674167,
2.5088811015245,2.53299182872568,2.55388883690921,2.59892722220135,2.60318389446238,
2.60571366671517,2.60765217013647,2.60972953080684,2.61299792841729,2.61680081734889,
2.62406474248904,2.66768826363348),.UNSPECIFIED.);
#1766=B_SPLINE_CURVE_WITH_KNOTS('',3,(#166527,#166528,#166529,#166530,#166531,
#166532,#166533,#166534,#166535,#166536,#166537,#166538,#166539,#166540,
#166541,#166542,#166543,#166544,#166545,#166546),.UNSPECIFIED.,.F.,.F.,
(4,2,2,2,2,2,2,2,2,4),(0.000649988982928049,0.0375152709071572,0.0412926030068312,
0.0433020300555975,0.0446072114830325,0.0458444148964173,0.0469177273846094,
0.0482917865179784,0.051132055185458,0.0747588911148556),.UNSPECIFIED.);
#1767=B_SPLINE_CURVE_WITH_KNOTS('',3,(#166552,#166553,#166554,#166555,#166556,
#166557,#166558,#166559,#166560,#166561),.UNSPECIFIED.,.F.,.F.,(4,3,3,4),
(120.689857252469,120.859210445387,120.962579625168,121.040544022956),
 .UNSPECIFIED.);
#1768=B_SPLINE_CURVE_WITH_KNOTS('',3,(#166562,#166563,#166564,#166565,#166566,
#166567,#166568,#166569,#166570,#166571),.UNSPECIFIED.,.F.,.F.,(4,1,1,1,
1,1,1,4),(114.756144714286,114.866191745616,115.865028195577,116.863864645539,
117.862701095501,118.861537545463,119.860373995425,120.689851223516),
 .UNSPECIFIED.);
#1769=B_SPLINE_CURVE_WITH_KNOTS('',3,(#166572,#166573,#166574,#166575,#166576,
#166577,#166578,#166579,#166580,#166581,#166582,#166583,#166584,#166585,
#166586,#166587,#166588,#166589,#166590,#166591,#166592,#166593,#166594,
#166595,#166596,#166597,#166598,#166599,#166600,#166601,#166602,#166603,
#166604,#166605,#166606,#166607,#166608,#166609,#166610,#166611,#166612,
#166613,#166614,#166615,#166616,#166617,#166618,#166619,#166620,#166621,
#166622,#166623,#166624,#166625,#166626,#166627,#166628,#166629,#166630,
#166631,#166632,#166633,#166634,#166635,#166636,#166637,#166638,#166639,
#166640,#166641,#166642,#166643,#166644,#166645,#166646,#166647,#166648,
#166649,#166650,#166651,#166652,#166653,#166654,#166655,#166656,#166657,
#166658,#166659,#166660,#166661,#166662,#166663,#166664,#166665,#166666,
#166667,#166668,#166669,#166670,#166671,#166672,#166673,#166674,#166675,
#166676,#166677,#166678,#166679,#166680,#166681,#166682,#166683,#166684,
#166685,#166686,#166687,#166688,#166689,#166690,#166691,#166692,#166693,
#166694,#166695,#166696,#166697,#166698,#166699,#166700,#166701,#166702,
#166703,#166704,#166705,#166706,#166707,#166708,#166709,#166710,#166711,
#166712,#166713,#166714,#166715,#166716,#166717,#166718,#166719,#166720,
#166721,#166722,#166723,#166724,#166725,#166726,#166727,#166728,#166729,
#166730,#166731,#166732,#166733,#166734,#166735,#166736,#166737,#166738,
#166739,#166740,#166741,#166742,#166743,#166744,#166745,#166746,#166747,
#166748,#166749,#166750,#166751,#166752,#166753,#166754,#166755,#166756,
#166757,#166758,#166759,#166760,#166761,#166762,#166763,#166764,#166765,
#166766,#166767,#166768,#166769,#166770,#166771,#166772,#166773,#166774,
#166775,#166776,#166777,#166778,#166779,#166780,#166781,#166782,#166783,
#166784,#166785,#166786,#166787,#166788,#166789),.UNSPECIFIED.,.F.,.F.,
(4,2,2,2,2,2,2,2,2,2,2,2,2,2,2,2,2,2,2,2,2,2,2,2,2,2,2,2,2,2,2,2,2,2,2,
2,2,2,2,2,2,2,2,2,2,2,2,2,2,2,2,2,2,2,2,2,2,2,2,2,2,2,2,2,2,2,2,2,2,2,2,
2,2,2,2,2,2,2,2,2,2,2,2,2,2,2,2,2,2,2,2,2,2,2,2,2,2,2,2,2,2,2,2,2,2,2,2,
2,4),(0.0747588911148556,0.087979694588596,0.109399136949241,0.136182140554699,
0.146436035987435,0.149706925655296,0.151785020597418,0.153723617536559,
0.156252665620082,0.160506269737635,0.193185982491467,0.22255610653982,
0.244174291645429,0.254295267426268,0.256485238129221,0.257733385334679,
0.258805387235881,0.26016385040786,0.26283591418482,0.28021709369287,0.329256334993405,
0.347303221259107,0.354572452419847,0.360002124569805,0.362567486827097,
0.364504846715067,0.366333003885582,0.368880952611567,0.375561837111131,
0.430975921106836,0.455320546238687,0.466218593280985,0.468466939481635,
0.469718052812365,0.470789803387546,0.472144360538783,0.474886251973298,
0.493334149644452,0.537461144228889,0.565331953351833,0.571665374198063,
0.574356996676347,0.576315555506733,0.57811169641977,0.580996255765975,
0.587999994025098,0.639383233690721,0.666515232559005,0.678128411701344,
0.680418179427137,0.681678323015426,0.682749327388064,0.684092175553081,
0.686691246643468,0.702216444472666,0.708761400960079,0.722633915488646,
0.755493977812072,0.772056477515175,0.782367900486531,0.785616704542271,
0.787690086444634,0.789630821229254,0.792172066640925,0.796467222035025,
0.831578342181658,0.880465467159598,0.89028865354969,0.892468511707725,
0.893704743449463,0.894778444650492,0.896154609205564,0.899004737472686,
0.935374661653975,0.989163067608613,0.995619120739391,0.998331688515185,
1.00029418264342,1.00208615606779,1.00494708242994,1.01180636174837,1.06524496581856,
1.09093521918544,1.10218661822474,1.10445603590278,1.10571184448875,1.10678332906235,
1.10813208207245,1.1107581471268,1.1269223330942,1.1775803274199,1.20199431100506,
1.20789433150569,1.21051039586907,1.21245609416164,1.21427049060166,1.21676509944741,
1.22311494402584,1.28150392542795,1.30395458582152,1.31433180589374,1.31654821041432,
1.31779249621548,1.31886522030498,1.32022981461843,1.32240322478293,1.33389992718014,
1.38263552906857,1.40832427926634),.UNSPECIFIED.);
#1770=B_SPLINE_CURVE_WITH_KNOTS('',3,(#166795,#166796,#166797,#166798,#166799,
#166800,#166801,#166802),.UNSPECIFIED.,.F.,.F.,(4,2,2,4),(2.59385008432844,
2.59859935883543,2.62663692859619,2.66832834108701),.UNSPECIFIED.);
#1771=B_SPLINE_CURVE_WITH_KNOTS('',3,(#166803,#166804,#166805,#166806,#166807,
#166808,#166809,#166810,#166811,#166812,#166813,#166814,#166815,#166816,
#166817,#166818,#166819,#166820,#166821,#166822,#166823,#166824,#166825,
#166826,#166827,#166828,#166829,#166830,#166831,#166832,#166833,#166834,
#166835,#166836,#166837,#166838,#166839,#166840,#166841,#166842,#166843,
#166844,#166845,#166846,#166847,#166848,#166849,#166850,#166851,#166852,
#166853,#166854,#166855,#166856,#166857,#166858,#166859,#166860,#166861,
#166862,#166863,#166864,#166865,#166866,#166867,#166868,#166869,#166870,
#166871,#166872,#166873,#166874,#166875,#166876,#166877,#166878,#166879,
#166880,#166881,#166882,#166883,#166884,#166885,#166886,#166887,#166888,
#166889,#166890,#166891,#166892,#166893,#166894,#166895,#166896,#166897,
#166898,#166899,#166900,#166901,#166902,#166903,#166904,#166905,#166906,
#166907,#166908,#166909,#166910,#166911,#166912,#166913,#166914,#166915,
#166916,#166917,#166918,#166919,#166920,#166921,#166922,#166923,#166924,
#166925,#166926,#166927,#166928,#166929,#166930,#166931,#166932,#166933,
#166934,#166935,#166936,#166937,#166938,#166939,#166940,#166941,#166942,
#166943,#166944,#166945,#166946,#166947,#166948,#166949,#166950,#166951,
#166952,#166953,#166954,#166955,#166956,#166957,#166958,#166959,#166960,
#166961,#166962,#166963,#166964,#166965,#166966,#166967,#166968,#166969,
#166970,#166971,#166972,#166973,#166974,#166975,#166976,#166977,#166978,
#166979,#166980),.UNSPECIFIED.,.F.,.F.,(4,3,3,3,3,3,3,3,3,3,3,3,3,3,3,3,
3,3,3,3,3,3,3,3,3,3,3,3,3,3,3,3,3,3,3,3,3,3,3,3,3,3,3,3,3,3,3,3,3,3,3,3,
3,3,3,3,3,3,3,4),(121.040544022956,121.143685231131,121.246752684529,121.349780436244,
121.452802487907,121.55592611181,121.659098574575,121.762462086372,121.858046895349,
121.961441632397,122.064682914512,122.167802879905,122.270857448114,122.373880656472,
122.476906499144,122.580039265923,122.683228357333,122.786600350714,122.856883345311,
122.960278082359,123.063519364473,123.166639329865,123.269693898074,123.372717106431,
123.475742949104,123.578875715881,123.682064807291,123.785436800672,123.855719795272,
123.95911453232,124.062355814435,124.165475779827,124.268530348036,124.371553556394,
124.474579399066,124.577712165844,124.680901257254,124.784273250636,124.854556245234,
124.957950982282,125.061192264397,125.16431222979,125.267366797999,125.370390006357,
125.473415849029,125.576548615808,125.679737707218,125.783109700599,125.853392695196,
125.956787432244,126.060028714359,126.163148679751,126.26620324796,126.369226456318,
126.472252298991,126.575385065769,126.678574157179,126.78194615056,126.852229145158,
126.973042559648),.UNSPECIFIED.);
#1772=B_SPLINE_CURVE_WITH_KNOTS('',3,(#166982,#166983,#166984,#166985,#166986,
#166987,#166988,#166989,#166990,#166991,#166992,#166993,#166994,#166995,
#166996,#166997,#166998,#166999,#167000,#167001,#167002,#167003,#167004,
#167005,#167006,#167007,#167008,#167009,#167010,#167011,#167012,#167013,
#167014,#167015,#167016,#167017,#167018,#167019,#167020,#167021,#167022,
#167023,#167024,#167025,#167026,#167027,#167028,#167029,#167030,#167031,
#167032,#167033,#167034,#167035,#167036,#167037,#167038,#167039,#167040,
#167041,#167042,#167043,#167044,#167045,#167046,#167047,#167048,#167049,
#167050,#167051,#167052,#167053,#167054,#167055,#167056,#167057,#167058,
#167059,#167060,#167061,#167062,#167063,#167064,#167065,#167066,#167067,
#167068,#167069,#167070,#167071,#167072,#167073,#167074,#167075,#167076,
#167077,#167078,#167079,#167080,#167081,#167082,#167083,#167084,#167085,
#167086,#167087,#167088,#167089,#167090,#167091,#167092,#167093,#167094,
#167095,#167096,#167097,#167098,#167099,#167100,#167101,#167102,#167103,
#167104,#167105,#167106,#167107,#167108,#167109,#167110,#167111,#167112,
#167113,#167114,#167115,#167116,#167117,#167118,#167119,#167120,#167121,
#167122,#167123,#167124,#167125,#167126,#167127,#167128,#167129,#167130,
#167131,#167132,#167133,#167134,#167135,#167136,#167137,#167138,#167139,
#167140,#167141,#167142,#167143,#167144,#167145,#167146,#167147,#167148,
#167149,#167150,#167151,#167152,#167153,#167154,#167155,#167156,#167157,
#167158,#167159,#167160,#167161,#167162,#167163,#167164,#167165,#167166,
#167167,#167168,#167169,#167170,#167171,#167172,#167173,#167174,#167175,
#167176,#167177,#167178,#167179,#167180,#167181,#167182,#167183,#167184,
#167185,#167186,#167187,#167188,#167189,#167190,#167191,#167192,#167193,
#167194,#167195,#167196,#167197,#167198,#167199),.UNSPECIFIED.,.F.,.F.,
(4,2,2,2,2,2,2,2,2,2,2,2,2,2,2,2,2,2,2,2,2,2,2,2,2,2,2,2,2,2,2,2,2,2,2,
2,2,2,2,2,2,2,2,2,2,2,2,2,2,2,2,2,2,2,2,2,2,2,2,2,2,2,2,2,2,2,2,2,2,2,2,
2,2,2,2,2,2,2,2,2,2,2,2,2,2,2,2,2,2,2,2,2,2,2,2,2,2,2,2,2,2,2,2,2,2,2,2,
2,4),(1.40832427926634,1.4158388062147,1.42010266029481,1.42263495150552,
1.42457437188948,1.42665172707618,1.42991803767986,1.44038109885889,1.45728205103867,
1.49511040246738,1.52518594762253,1.52810053893145,1.52948931560261,1.53056429223976,
1.53179241090507,1.53393533718452,1.54323149310023,1.56207803469736,1.60247851019985,
1.61474060438569,1.62934644710789,1.63313472526375,1.63534971493536,1.63726197419843,
1.63959700388483,1.64404692630448,1.6749596348227,1.72180634881348,1.73760400443668,
1.74021648824691,1.74156237286273,1.74263374219591,1.74389193216911,1.7461720482291,
1.75760863207442,1.78402405523123,1.83638779062094,1.84332622545897,1.84620030356327,
1.8479947631746,1.84995537216268,1.85265689086746,1.85904674336266,1.88738501485849,
1.93728474532696,1.94991457736624,1.95215082810244,1.9535344518334,1.95460896006765,
1.95584049504417,1.9579986935857,1.96750734347849,2.01664197498015,2.05182812617918,
2.05612448612284,2.05866624811658,2.06060725355324,2.06268080361921,2.06592961736213,
2.07623884721228,2.09279801573864,2.12568557287272,2.13955174482702,2.1461141664972,
2.16166404073964,2.16426446477404,2.16560770326363,2.16667885498645,2.16793898646776,
2.17022824628745,2.18182910816754,2.20890610924678,2.2603362859139,2.26733504531375,
2.27021900055765,2.27201519475415,2.27397416006816,2.27666696716224,2.28300607532969,
2.31092439298894,2.35693401362682,2.35802620661315,2.37367486915399,2.37627933554951,
2.37762344466943,2.37869464608864,2.37995408655873,2.38224017082084,2.39378430044301,
2.42063176551538,2.47235791712428,2.47935400996171,2.4822375149983,2.48403362086753,
2.48585454824163,2.48840725970004,2.49399834014362,2.50150583662065,2.5204175318765,
2.54640017272129,2.58249627838875,2.58727554921537,2.58902572115793,2.59005302557666,
2.59114431881853,2.5926483382996,2.59619385941298,2.6289385996989,2.66749524589182),
 .UNSPECIFIED.);
#1773=B_SPLINE_CURVE_WITH_KNOTS('',3,(#167200,#167201,#167202,#167203,#167204,
#167205,#167206,#167207,#167208,#167209,#167210,#167211,#167212,#167213,
#167214,#167215,#167216,#167217,#167218,#167219,#167220,#167221),
 .UNSPECIFIED.,.F.,.F.,(4,2,2,2,2,2,2,2,2,2,4),(0.000768645035296635,0.0217310010489876,
0.0248341253626711,0.0269704391246487,0.0287696835339234,0.0306848756723677,
0.0330688196914889,0.0367500933377631,0.0545891744943505,0.0729777540908564,
0.0751664254368708),.UNSPECIFIED.);
#1774=B_SPLINE_CURVE_WITH_KNOTS('',3,(#167226,#167227,#167228,#167229,#167230,
#167231,#167232,#167233,#167234,#167235,#167236,#167237,#167238,#167239,
#167240,#167241,#167242,#167243,#167244,#167245,#167246,#167247,#167248,
#167249,#167250,#167251,#167252,#167253,#167254,#167255,#167256,#167257,
#167258,#167259,#167260,#167261,#167262,#167263,#167264,#167265,#167266,
#167267,#167268,#167269,#167270,#167271,#167272,#167273,#167274,#167275,
#167276,#167277,#167278,#167279,#167280,#167281,#167282,#167283,#167284,
#167285,#167286,#167287,#167288,#167289,#167290,#167291,#167292,#167293,
#167294,#167295,#167296,#167297,#167298,#167299,#167300,#167301,#167302,
#167303,#167304,#167305,#167306,#167307,#167308,#167309,#167310,#167311,
#167312,#167313,#167314,#167315,#167316,#167317,#167318,#167319,#167320,
#167321,#167322,#167323,#167324,#167325,#167326,#167327,#167328,#167329,
#167330,#167331,#167332,#167333,#167334,#167335,#167336,#167337,#167338,
#167339,#167340,#167341,#167342,#167343,#167344,#167345,#167346,#167347,
#167348,#167349,#167350,#167351,#167352,#167353,#167354,#167355,#167356,
#167357,#167358,#167359,#167360,#167361,#167362,#167363,#167364,#167365,
#167366,#167367,#167368,#167369,#167370,#167371,#167372,#167373,#167374,
#167375,#167376,#167377,#167378,#167379,#167380,#167381,#167382,#167383,
#167384,#167385,#167386,#167387,#167388,#167389,#167390,#167391,#167392,
#167393,#167394,#167395,#167396,#167397,#167398,#167399,#167400,#167401,
#167402,#167403,#167404,#167405,#167406,#167407,#167408,#167409,#167410,
#167411,#167412,#167413,#167414,#167415,#167416,#167417,#167418,#167419,
#167420,#167421,#167422,#167423,#167424,#167425,#167426,#167427,#167428,
#167429,#167430,#167431,#167432,#167433,#167434,#167435,#167436,#167437,
#167438,#167439,#167440,#167441,#167442,#167443,#167444,#167445,#167446,
#167447,#167448,#167449,#167450,#167451,#167452,#167453,#167454,#167455),
 .UNSPECIFIED.,.F.,.F.,(4,2,2,2,2,2,2,2,2,2,2,2,2,2,2,2,2,2,2,2,2,2,2,2,
2,2,2,2,2,2,2,2,2,2,2,2,2,2,2,2,2,2,2,2,2,2,2,2,2,2,2,2,2,2,2,2,2,2,2,2,
2,2,2,2,2,2,2,2,2,2,2,2,2,2,2,2,2,2,2,2,2,2,2,2,2,2,2,2,2,2,2,2,2,2,2,2,
2,2,2,2,2,2,2,2,2,2,2,2,2,2,2,2,2,2,4),(1.25997501180952,1.2781789465602,
1.30768283917131,1.31209327376651,1.31442021416852,1.31614731222761,1.31830375361268,
1.32192660105968,1.33437740302623,1.38533839436569,1.4165482807573,1.4194614750814,
1.42085013634194,1.42192527693291,1.42315386621344,1.42529827720666,1.43461112346177,
1.48377031670444,1.51916083916367,1.52346020859321,1.52600300379715,1.52794436810435,
1.53001788467215,1.53326577592756,1.54356475303071,1.56010049196427,1.59297093809217,
1.60449684565962,1.61425394219995,1.6160834713369,1.62921411944707,1.63147619039573,
1.63286761083593,1.63394297443524,1.63516968294175,1.6373058256739,1.64650641360302,
1.66505235444365,1.70908280759338,1.73177956170391,1.73573300667775,1.73820045845035,
1.74012482527639,1.74225316210225,1.74574938287702,1.75844095315729,1.80939893074747,
1.84061062632473,1.84352373068957,1.84491235031177,1.84598745923835,1.84721601297642,
1.84936036343403,1.85867296999624,1.90783082486616,1.94322016748382,1.94751940897756,
1.95006212902028,1.95200343623404,1.95407689210245,1.95732468886643,1.9676233712772,
1.98415864175162,2.01702813681136,2.05272380342247,2.05558630847344,2.05696502449738,
2.05803910557485,2.05927396579576,2.06144706787455,2.07116845650035,2.12012418868578,
2.1552559962964,2.15955187855519,2.1620935793153,2.16403466548044,2.16610842539875,
2.16935782602938,2.17967109375628,2.19623881795404,2.2291346267226,2.264743987593,
2.26761022074736,2.26898963847532,2.27006375378906,2.27129807574626,2.27346885319651,
2.28315728077931,2.33213897684789,2.36727839141135,2.37157423670341,2.37411588053553,
2.37605690303558,2.37813057536138,2.38137979786745,2.39169215565431,2.40825809022025,
2.47089938433272,2.47226076536006,2.47843448250944,2.48037288284897,2.48155570093292,
2.48258738047931,2.48400047045733,2.48701554544795,2.49111375097756,2.50139218337894,
2.52421476761476,2.57592759698011,2.58291151628283,2.58579342020861,2.58758953893425,
2.58954938172231,2.59224514258579,2.59385008432844),.UNSPECIFIED.);
#1775=B_SPLINE_CURVE_WITH_KNOTS('',3,(#167456,#167457,#167458,#167459,#167460,
#167461,#167462,#167463,#167464,#167465,#167466,#167467,#167468,#167469,
#167470,#167471,#167472,#167473,#167474,#167475,#167476,#167477,#167478,
#167479,#167480,#167481,#167482,#167483,#167484,#167485,#167486,#167487,
#167488,#167489,#167490,#167491,#167492,#167493,#167494,#167495,#167496,
#167497,#167498,#167499,#167500,#167501,#167502,#167503,#167504,#167505,
#167506,#167507,#167508,#167509,#167510,#167511,#167512,#167513,#167514,
#167515,#167516,#167517,#167518,#167519,#167520,#167521,#167522,#167523,
#167524,#167525,#167526,#167527,#167528,#167529,#167530,#167531,#167532,
#167533,#167534,#167535,#167536,#167537,#167538,#167539,#167540,#167541,
#167542,#167543,#167544,#167545,#167546,#167547,#167548,#167549,#167550,
#167551,#167552,#167553,#167554,#167555,#167556,#167557,#167558,#167559,
#167560,#167561,#167562,#167563,#167564,#167565,#167566,#167567,#167568,
#167569,#167570,#167571,#167572,#167573,#167574,#167575,#167576,#167577,
#167578,#167579,#167580,#167581,#167582,#167583,#167584,#167585,#167586,
#167587,#167588,#167589,#167590,#167591,#167592,#167593,#167594,#167595,
#167596,#167597,#167598,#167599,#167600,#167601,#167602,#167603,#167604,
#167605,#167606,#167607,#167608,#167609,#167610,#167611,#167612,#167613,
#167614,#167615,#167616,#167617,#167618,#167619,#167620,#167621,#167622,
#167623,#167624,#167625,#167626,#167627,#167628,#167629,#167630,#167631,
#167632,#167633,#167634,#167635,#167636,#167637,#167638,#167639,#167640,
#167641,#167642,#167643,#167644,#167645,#167646,#167647,#167648,#167649,
#167650,#167651,#167652,#167653,#167654,#167655,#167656,#167657,#167658,
#167659,#167660,#167661,#167662,#167663,#167664,#167665,#167666,#167667,
#167668,#167669,#167670,#167671,#167672,#167673,#167674,#167675,#167676,
#167677,#167678,#167679,#167680,#167681,#167682,#167683,#167684,#167685,
#167686,#167687,#167688,#167689),.UNSPECIFIED.,.F.,.F.,(4,2,2,2,2,2,2,2,
2,2,2,2,2,2,2,2,2,2,2,2,2,2,2,2,2,2,2,2,2,2,2,2,2,2,2,2,2,2,2,2,2,2,2,2,
2,2,2,2,2,2,2,2,2,2,2,2,2,2,2,2,2,2,2,2,2,2,2,2,2,2,2,2,2,2,2,2,2,2,2,2,
2,2,2,2,2,2,2,2,2,2,2,2,2,2,2,2,2,2,2,2,2,2,2,2,2,2,2,2,2,2,2,2,2,2,2,2,
4),(0.0751664254368708,0.121845955344527,0.131682137292399,0.133862665319429,
0.135098937946201,0.136172458199343,0.137548108280382,0.140396202121225,
0.176828797185436,0.209403310472754,0.225624337256069,0.232373911160273,
0.237516241657923,0.239979328300749,0.241820421564232,0.243647570729462,
0.246191314375334,0.252844260980652,0.308554353084904,0.3327085642093,0.343555926381325,
0.345801361990051,0.347051910603007,0.348123827059192,0.349479426759677,
0.351623526946022,0.362637199903487,0.413913723232091,0.442560878010676,
0.448987785534373,0.451695383130414,0.453656921841771,0.455449838961509,
0.458316220325194,0.46520904244774,0.518210971510428,0.544202176327027,
0.555530343689891,0.557804126181521,0.559060855862157,0.560132218997533,
0.561479664165487,0.564099783774063,0.580115853324613,0.58515641325212,
0.629885439006828,0.64840508235415,0.659579457989206,0.662923756175396,
0.665018220058885,0.666951401558858,0.669444265585323,0.673573516242521,
0.700875431160467,0.743135477132519,0.759411357262032,0.7678548497415,0.769932722873498,
0.771146409166725,0.772224103332976,0.773613375875094,0.775918769636958,
0.789939218927439,0.791301065984591,0.798313691139858,0.811988689662026,
0.844849708791797,0.861411252811406,0.871722501364627,0.874971474260879,
0.877045017688488,0.878985941435396,0.881527488775433,0.885823276629063,
0.920955665558956,0.969902203516858,0.97966107016502,0.981836679738371,
0.983072047071761,0.984145986284646,0.985523748320218,0.988381628690608,
1.01124176969533,1.02400706443002,1.05686282156235,1.07341556753015,1.08372313553391,
1.08697190544598,1.08904554928356,1.09098672857402,1.09352884366621,1.09782611376155,
1.13304085164816,1.18224625769595,1.19171023916762,1.19386546313084,1.19509642480876,
1.19617116604592,1.19755604375425,1.19979618151898,1.21249759832307,1.2348756064397,
1.26847944014398,1.29385667535051,1.2981273832955,1.30042491787518,1.30231799097671,
1.30455873716748,1.30845790255933,1.32436660850639,1.33458886721821,1.37387326870316,
1.40245749186511,1.40537004963331,1.40675860124106,1.40783374616902,1.40876564968185),
 .UNSPECIFIED.);
#1776=B_SPLINE_CURVE_WITH_KNOTS('',3,(#167695,#167696,#167697,#167698,#167699,
#167700,#167701,#167702,#167703,#167704,#167705,#167706,#167707,#167708,
#167709,#167710,#167711,#167712,#167713,#167714,#167715,#167716),
 .UNSPECIFIED.,.F.,.F.,(4,2,2,2,2,2,2,2,2,2,4),(2.59321272354364,2.59676257810928,
2.60140795147772,2.60313777369838,2.60416108640238,2.60525490880966,2.6067734902191,
2.61040446374374,2.61551550281731,2.62968314141178,2.66731559418949),
 .UNSPECIFIED.);
#1777=B_SPLINE_CURVE_WITH_KNOTS('',3,(#167717,#167718,#167719,#167720,#167721,
#167722,#167723,#167724,#167725,#167726,#167727,#167728,#167729,#167730,
#167731,#167732,#167733,#167734,#167735,#167736,#167737,#167738,#167739,
#167740,#167741,#167742,#167743,#167744,#167745,#167746,#167747,#167748,
#167749,#167750,#167751,#167752,#167753,#167754,#167755,#167756,#167757,
#167758,#167759,#167760,#167761,#167762,#167763,#167764,#167765,#167766,
#167767,#167768,#167769,#167770,#167771,#167772,#167773,#167774,#167775,
#167776,#167777,#167778,#167779,#167780,#167781,#167782,#167783,#167784,
#167785,#167786,#167787,#167788,#167789,#167790,#167791,#167792,#167793,
#167794,#167795,#167796,#167797,#167798,#167799,#167800,#167801,#167802,
#167803,#167804,#167805,#167806,#167807,#167808,#167809,#167810,#167811,
#167812,#167813,#167814,#167815,#167816,#167817,#167818,#167819,#167820,
#167821,#167822,#167823,#167824,#167825,#167826,#167827,#167828,#167829,
#167830,#167831,#167832,#167833,#167834,#167835,#167836,#167837,#167838,
#167839,#167840,#167841,#167842,#167843,#167844,#167845,#167846,#167847,
#167848,#167849,#167850,#167851,#167852,#167853,#167854,#167855,#167856,
#167857,#167858,#167859,#167860,#167861,#167862,#167863,#167864,#167865,
#167866,#167867,#167868,#167869,#167870,#167871,#167872,#167873,#167874,
#167875,#167876,#167877,#167878,#167879,#167880,#167881,#167882,#167883,
#167884,#167885,#167886,#167887,#167888,#167889,#167890,#167891,#167892,
#167893,#167894,#167895,#167896,#167897,#167898,#167899,#167900,#167901,
#167902,#167903,#167904,#167905,#167906,#167907,#167908,#167909,#167910,
#167911,#167912,#167913,#167914,#167915,#167916,#167917,#167918,#167919,
#167920,#167921,#167922,#167923,#167924,#167925,#167926,#167927,#167928,
#167929,#167930,#167931,#167932,#167933,#167934,#167935,#167936,#167937,
#167938,#167939,#167940,#167941,#167942,#167943,#167944),.UNSPECIFIED.,
 .F.,.F.,(4,2,2,2,2,2,2,2,2,2,2,2,2,2,2,2,2,2,2,2,2,2,2,2,2,2,2,2,2,2,2,
2,2,2,2,2,2,2,2,2,2,2,2,2,2,2,2,2,2,2,2,2,2,2,2,2,2,2,2,2,2,2,2,2,2,2,2,
2,2,2,2,2,2,2,2,2,2,2,2,2,2,2,2,2,2,2,2,2,2,2,2,2,2,2,2,2,2,2,2,2,2,2,2,
2,2,2,2,2,2,2,2,2,2,4),(0.000704182981740823,0.025717628190997,0.0359848718289681,
0.03906358535599,0.0411898775184007,0.0432710250581594,0.0452083866403788,
0.0477299960570225,0.0519581881395003,0.0833517469152109,0.108702852437119,
0.13665961579832,0.145914702164939,0.148054314070839,0.14928151697485,0.150356340023211,
0.151745763369213,0.15400201116064,0.167029448661604,0.188640582450494,
0.215343078701711,0.236968499593147,0.245192539158449,0.251206096285135,
0.253833976559155,0.25579066677997,0.257588990735752,0.260485650014074,
0.267562362499414,0.317897166975829,0.355567136046225,0.359165334448484,
0.360678274131995,0.361771027273397,0.362795721022258,0.364532931729908,
0.369227564009042,0.410091366748055,0.456727973956269,0.46312059249124,
0.465822275557283,0.467782639577261,0.469576627552671,0.472449398259115,
0.479381808821687,0.531832612605671,0.558205643024063,0.56963007483175,
0.571909234692174,0.573167077321925,0.5742382634427,0.57558405490196,0.578196760828911,
0.594049725598797,0.598811519778327,0.614071539478433,0.646947531783168,
0.663529264405269,0.673849382583489,0.677099182913534,0.679172782068762,
0.681113426283792,0.683654129139571,0.687947417560457,0.730346714312759,
0.759401303224733,0.774125195971442,0.782017724573933,0.784049651902801,
0.785253088016879,0.786333171619793,0.787740579140585,0.790108030106355,
0.805546523747528,0.812261789130739,0.826060561359919,0.858921261247343,
0.875483540258535,0.885794984344839,0.889043879387732,0.89111733961951,
0.893058161954385,0.895599542539845,0.899894972422117,0.935014387027832,
0.98392412590432,0.99372333135132,0.995901622710922,0.997137542667392,0.998211341754463,
0.999588113337181,1.00244115227971,1.02511108920957,1.03806701684262,1.07092292722108,
1.0874769840124,1.09778500748103,1.10103372883791,1.103107295508,1.10504837011985,
1.10759030131288,1.11188715558912,1.14708420180628,1.19623358777709,1.20575895584113,
1.20791844347136,1.2091503073185,1.21022484475367,1.21160815732742,1.21384321294934,
1.22644914254929,1.23298243684644,1.23811588181959,1.25997501180952),
 .UNSPECIFIED.);
#1778=B_SPLINE_CURVE_WITH_KNOTS('',3,(#167946,#167947,#167948,#167949,#167950,
#167951,#167952,#167953,#167954,#167955,#167956,#167957,#167958,#167959,
#167960,#167961,#167962,#167963,#167964,#167965,#167966,#167967,#167968,
#167969,#167970,#167971,#167972,#167973,#167974,#167975,#167976,#167977,
#167978,#167979,#167980,#167981,#167982,#167983,#167984,#167985,#167986,
#167987,#167988,#167989,#167990,#167991,#167992,#167993,#167994,#167995,
#167996,#167997,#167998,#167999,#168000,#168001,#168002,#168003,#168004,
#168005,#168006,#168007,#168008,#168009,#168010,#168011,#168012,#168013,
#168014,#168015,#168016,#168017,#168018,#168019,#168020,#168021,#168022,
#168023,#168024,#168025,#168026,#168027,#168028,#168029,#168030,#168031,
#168032,#168033,#168034,#168035,#168036,#168037,#168038,#168039,#168040,
#168041,#168042,#168043,#168044,#168045,#168046,#168047,#168048,#168049,
#168050,#168051,#168052,#168053,#168054,#168055,#168056,#168057,#168058,
#168059,#168060,#168061,#168062,#168063,#168064,#168065,#168066,#168067,
#168068,#168069,#168070,#168071,#168072,#168073,#168074,#168075,#168076,
#168077,#168078,#168079,#168080,#168081,#168082,#168083,#168084,#168085,
#168086,#168087,#168088,#168089,#168090,#168091,#168092,#168093,#168094,
#168095,#168096,#168097,#168098,#168099,#168100,#168101,#168102,#168103,
#168104,#168105,#168106,#168107,#168108,#168109,#168110,#168111,#168112,
#168113,#168114,#168115,#168116,#168117,#168118,#168119,#168120,#168121,
#168122,#168123,#168124,#168125,#168126,#168127,#168128,#168129,#168130,
#168131,#168132,#168133,#168134,#168135,#168136,#168137,#168138,#168139,
#168140,#168141,#168142,#168143,#168144,#168145,#168146,#168147,#168148,
#168149,#168150,#168151,#168152,#168153,#168154,#168155,#168156,#168157,
#168158,#168159,#168160,#168161,#168162,#168163,#168164,#168165,#168166,
#168167,#168168,#168169,#168170,#168171,#168172,#168173,#168174,#168175,
#168176,#168177),.UNSPECIFIED.,.F.,.F.,(4,2,2,2,2,2,2,2,2,2,2,2,2,2,2,2,
2,2,2,2,2,2,2,2,2,2,2,2,2,2,2,2,2,2,2,2,2,2,2,2,2,2,2,2,2,2,2,2,2,2,2,2,
2,2,2,2,2,2,2,2,2,2,2,2,2,2,2,2,2,2,2,2,2,2,2,2,2,2,2,2,2,2,2,2,2,2,2,2,
2,2,2,2,2,2,2,2,2,2,2,2,2,2,2,2,2,2,2,2,2,2,2,2,2,2,2,4),(1.40876564968185,
1.40906244022885,1.41120726800264,1.42052554231052,1.46970202397115,1.5050712140085,
1.50937039427449,1.51191315663174,1.51385454135423,1.515928123814,1.51917621027683,
1.52947658062611,1.54601529218143,1.57356209642858,1.58970472045944,1.60078604712632,
1.61502103630848,1.61733761851502,1.61873029225954,1.61980856900322,1.62102062135248,
1.62309056749968,1.63143339162205,1.64741594131852,1.68973078454812,1.71734618386345,
1.72148384944831,1.7239794219376,1.72591328751353,1.72800707843134,1.73134723872194,
1.74247911383865,1.76090129375285,1.80769700377346,1.81248095721591,1.82701279929761,
1.82934290764825,1.83073956473504,1.83181838361534,1.83302820823886,1.83508805560075,
1.84330745271654,1.8589384169442,1.9007140705049,1.9293168194412,1.93348063663692,
1.93598391032542,1.93791897929598,1.94000933801229,1.9433338187686,1.95431945620387,
1.97240346137979,2.02247902304394,2.03890900988,2.04154614361546,2.04289744429846,
2.04396931159355,2.04522367799794,2.04748570091486,2.05860471830522,2.08377710415533,
2.13794821256296,2.14474594974472,2.14759707900135,2.14938756027183,2.15135218195495,
2.15407462077514,2.160587350901,2.18995687257223,2.23282297953381,2.25087240414281,
2.25356874959489,2.25493267721593,2.25600547090369,2.25725052298043,2.25946996388073,
2.26989206621916,2.29249681398209,2.35060633464067,2.35699003053181,2.35949049399086,
2.3613065689382,2.36325164626465,2.3658626526649,2.37173323864884,2.39592146672386,
2.44361404677803,2.46288490292848,2.46565407641264,2.46701432736083,2.46805600265418,
2.46806008033713,2.46806408942824,2.46806803122212,2.46807190727129,2.4680755060714,
2.4680790912502,2.46808266308603,2.46808622159869,2.46808976703347,2.46931345131289,
2.47062483679419,2.47264882762886,2.47646415089008,2.48574693661712,2.52369343304925,
2.53806500336148,2.56552438768444,2.56965801232864,2.57215240472521,2.57408610132007,
2.57618045330948,2.57952311983,2.59067836207953,2.60915478976905,2.66836429282343),
 .UNSPECIFIED.);
#1779=B_SPLINE_CURVE_WITH_KNOTS('',3,(#168178,#168179,#168180,#168181,#168182,
#168183,#168184,#168185,#168186,#168187,#168188,#168189,#168190,#168191,
#168192,#168193,#168194,#168195,#168196,#168197,#168198,#168199),
 .UNSPECIFIED.,.F.,.F.,(4,2,2,2,2,2,2,2,2,2,4),(0.000810719349047726,0.00554260972535774,
0.00881069122763486,0.0102445713069489,0.0113189801030348,0.0123417965676871,
0.0133649983883814,0.0148060144441036,0.0186526135973435,0.0263910041242044,
0.0750784321551894),.UNSPECIFIED.);
#1780=B_SPLINE_CURVE_WITH_KNOTS('',3,(#168204,#168205,#168206,#168207,#168208,
#168209,#168210,#168211,#168212,#168213,#168214,#168215,#168216,#168217,
#168218,#168219,#168220,#168221,#168222,#168223,#168224,#168225,#168226,
#168227,#168228,#168229,#168230,#168231,#168232,#168233,#168234,#168235,
#168236,#168237,#168238,#168239,#168240,#168241,#168242,#168243,#168244,
#168245,#168246,#168247,#168248,#168249,#168250,#168251,#168252,#168253,
#168254,#168255,#168256,#168257,#168258,#168259,#168260,#168261,#168262,
#168263,#168264,#168265,#168266,#168267,#168268,#168269,#168270,#168271,
#168272,#168273,#168274,#168275,#168276,#168277,#168278,#168279,#168280,
#168281,#168282,#168283,#168284,#168285,#168286,#168287,#168288,#168289,
#168290,#168291,#168292,#168293,#168294,#168295,#168296,#168297,#168298,
#168299,#168300,#168301,#168302,#168303,#168304,#168305,#168306,#168307,
#168308,#168309,#168310,#168311,#168312,#168313,#168314,#168315,#168316,
#168317,#168318,#168319,#168320,#168321,#168322,#168323,#168324,#168325,
#168326,#168327,#168328,#168329,#168330,#168331,#168332,#168333,#168334,
#168335,#168336,#168337,#168338,#168339,#168340,#168341,#168342,#168343,
#168344,#168345,#168346,#168347,#168348,#168349,#168350,#168351,#168352,
#168353,#168354,#168355,#168356,#168357,#168358,#168359,#168360,#168361,
#168362,#168363,#168364,#168365,#168366,#168367,#168368,#168369,#168370,
#168371,#168372,#168373,#168374,#168375,#168376,#168377,#168378,#168379,
#168380,#168381,#168382,#168383,#168384,#168385,#168386,#168387,#168388,
#168389,#168390,#168391,#168392,#168393,#168394,#168395,#168396,#168397,
#168398,#168399,#168400,#168401,#168402,#168403,#168404,#168405,#168406,
#168407,#168408,#168409,#168410,#168411,#168412,#168413,#168414,#168415,
#168416,#168417,#168418,#168419,#168420,#168421,#168422,#168423,#168424,
#168425,#168426,#168427,#168428,#168429,#168430,#168431,#168432,#168433),
 .UNSPECIFIED.,.F.,.F.,(4,2,2,2,2,2,2,2,2,2,2,2,2,2,2,2,2,2,2,2,2,2,2,2,
2,2,2,2,2,2,2,2,2,2,2,2,2,2,2,2,2,2,2,2,2,2,2,2,2,2,2,2,2,2,2,2,2,2,2,2,
2,2,2,2,2,2,2,2,2,2,2,2,2,2,2,2,2,2,2,2,2,2,2,2,2,2,2,2,2,2,2,2,2,2,2,2,
2,2,2,2,2,2,2,2,2,2,2,2,2,2,2,2,2,2,4),(1.25962401162403,1.26430974686983,
1.30525389854892,1.32773367756853,1.33039711422683,1.33173595952838,1.33270394114661,
1.33392756104424,1.33605009385992,1.34506885777096,1.36305411295081,1.41326996295484,
1.43107393322947,1.4347534136824,1.437137055044,1.43905255572398,1.44123132513247,
1.44495617516341,1.46036268422653,1.5116976762596,1.53937698828192,1.54228396149099,
1.54367128031833,1.54474613001321,1.54597522474859,1.54812248357969,1.55747820401669,
1.60674401211132,1.64196762190877,1.64626431184035,1.6488061194656,1.65074707361159,
1.65282048538134,1.65606890812334,1.66637542844875,1.68292884799442,1.7158108880148,
1.72925743961491,1.73684334193375,1.75184032035586,1.75418981295129,1.75559200684074,
1.7566714028084,1.75787776328051,1.75992267393493,1.76796661948303,1.78310657436369,
1.82281314578867,1.85404667218651,1.85827194568919,1.86079294472355,1.86273048562428,
1.86481246113277,1.8681000653812,1.87875349925591,1.8960818523767,1.94430089592049,
1.94860187229289,1.95167182499473,1.96405441542428,1.96627741309421,1.96765698675116,
1.96873102171676,1.96996502397064,1.97213469744821,1.98180935212029,2.03079696332603,
2.06593626548011,2.07023171975053,2.0727731185893,2.07471394613278,2.07678740255964,
2.08003627086668,2.09034737039031,2.10691115606774,2.13980106738308,2.15412310478184,
2.15979001781808,2.1757365431188,2.17835279667591,2.17969939104971,2.1807706760656,
2.18202801382229,2.18430466643489,2.19568412361328,2.22187539247344,2.2745466783258,
2.28146129242589,2.28433122035439,2.28612475724525,2.28808569654836,2.29079011932666,
2.29719838256437,2.30603771755433,2.35731649014562,2.38733951594719,2.39025396021666,
2.39164264936553,2.392717550224,2.39394557333261,2.39608831184729,2.40538332880179,
2.42422703132016,2.47041776955285,2.47187665102907,2.49090040361457,2.49466012115544,
2.4970683558831,2.49898594683945,2.50078321080397,2.50387581650965,2.51342015358757,
2.52841976651408,2.55071276904625,2.59321272354364),.UNSPECIFIED.);
#1781=B_SPLINE_CURVE_WITH_KNOTS('',3,(#168434,#168435,#168436,#168437,#168438,
#168439,#168440,#168441,#168442,#168443,#168444,#168445,#168446,#168447,
#168448,#168449,#168450,#168451,#168452,#168453,#168454,#168455,#168456,
#168457,#168458,#168459,#168460,#168461,#168462,#168463,#168464,#168465,
#168466,#168467,#168468,#168469,#168470,#168471,#168472,#168473,#168474,
#168475,#168476,#168477,#168478,#168479,#168480,#168481,#168482,#168483,
#168484,#168485,#168486,#168487,#168488,#168489,#168490,#168491,#168492,
#168493,#168494,#168495,#168496,#168497,#168498,#168499,#168500,#168501,
#168502,#168503,#168504,#168505,#168506,#168507,#168508,#168509,#168510,
#168511,#168512,#168513,#168514,#168515,#168516,#168517,#168518,#168519,
#168520,#168521,#168522,#168523,#168524,#168525,#168526,#168527,#168528,
#168529,#168530,#168531,#168532,#168533,#168534,#168535,#168536,#168537,
#168538,#168539,#168540,#168541,#168542,#168543,#168544,#168545,#168546,
#168547,#168548,#168549,#168550,#168551,#168552,#168553,#168554,#168555,
#168556,#168557,#168558,#168559,#168560,#168561,#168562,#168563,#168564,
#168565,#168566,#168567,#168568,#168569,#168570,#168571,#168572,#168573,
#168574,#168575,#168576,#168577,#168578,#168579,#168580,#168581,#168582,
#168583,#168584,#168585,#168586,#168587,#168588,#168589,#168590,#168591,
#168592,#168593,#168594,#168595,#168596,#168597,#168598,#168599,#168600,
#168601,#168602,#168603,#168604,#168605,#168606,#168607,#168608,#168609,
#168610,#168611,#168612,#168613,#168614,#168615,#168616,#168617,#168618,
#168619,#168620,#168621,#168622,#168623,#168624,#168625,#168626,#168627,
#168628,#168629,#168630,#168631,#168632,#168633,#168634,#168635,#168636,
#168637,#168638,#168639,#168640,#168641,#168642,#168643,#168644,#168645,
#168646,#168647,#168648,#168649,#168650,#168651,#168652,#168653,#168654,
#168655,#168656,#168657,#168658,#168659,#168660,#168661,#168662,#168663,
#168664,#168665,#168666,#168667,#168668,#168669),.UNSPECIFIED.,.F.,.F.,
(4,2,2,2,2,2,2,2,2,2,2,2,2,2,2,2,2,2,2,2,2,2,2,2,2,2,2,2,2,2,2,2,2,2,2,
2,2,2,2,2,2,2,2,2,2,2,2,2,2,2,2,2,2,2,2,2,2,2,2,2,2,2,2,2,2,2,2,2,2,2,2,
2,2,2,2,2,2,2,2,2,2,2,2,2,2,2,2,2,2,2,2,2,2,2,2,2,2,2,2,2,2,2,2,2,2,2,2,
2,2,2,2,2,2,2,2,2,2,4),(0.0750784321551894,0.0856872623994721,0.102193393147575,
0.112478518569802,0.115723726458095,0.117795941871022,0.119736378108385,
0.122278377924875,0.12657737730363,0.170030212772573,0.206390717145988,
0.215473289989933,0.219229765834113,0.221231249014688,0.22253308265916,
0.22374714081406,0.224790570685267,0.226140989918893,0.228775973475969,
0.245124041647403,0.289987075516811,0.319112007183808,0.325594883103514,
0.328311510938096,0.330274343106106,0.332064843634442,0.334919559901776,
0.34174405124641,0.395569126131839,0.420976331839343,0.432153467138812,
0.434418128315438,0.435672693654804,0.436743963674678,0.438093525868189,
0.440724353832407,0.456997756690263,0.507260214488163,0.525272304700002,
0.536226338249603,0.539546395202698,0.541635149565268,0.543569540359618,
0.546073074719094,0.55023983799993,0.579007410580277,0.620668305417106,
0.636259006936096,0.644462203559628,0.646520103232366,0.64772915482517,
0.648807545384551,0.650203973910826,0.652534381872989,0.6670915941988,0.675376366596123,
0.688562202379701,0.72140976150465,0.74414487954246,0.749822061529322,0.752397424511272,
0.75433626897467,0.7561613738279,0.75869792794741,0.765306350934032,0.821450195604848,
0.845310809628617,0.856078281621258,0.858318666635289,0.859568018740797,
0.860639907305439,0.861996752433854,0.864661200746954,0.881832375376879,
0.927325018123464,0.955180081594329,0.96151148229728,0.964202698482331,
0.966161128059916,0.96795726576907,0.970842073309733,0.977847705744469,
1.02918016800007,1.05634711330801,1.0679686894587,1.07025886091832,1.07151906264762,
1.07259001773328,1.07393267901382,1.07653102435352,1.09204096082917,1.09861454965795,
1.13998978460787,1.16725276669186,1.17351215268915,1.17619110497389,1.17814741784952,
1.17994635503659,1.18284612572453,1.18994112421196,1.23956648931162,1.27794079158437,
1.28152639688112,1.28303722127884,1.28412963324536,1.28515495154683,1.28689523444239,
1.29160989292968,1.33201667301647,1.33390594999482,1.37772798415467,1.38494942829632,
1.38787046320037,1.38967335423326,1.39162670736977,1.39428857074071,1.40044887524773,
1.40839008782515),.UNSPECIFIED.);
#1782=B_SPLINE_CURVE_WITH_KNOTS('',3,(#168675,#168676,#168677,#168678),
 .UNSPECIFIED.,.F.,.F.,(4,4),(152.105783788367,152.455231433536),
 .UNSPECIFIED.);
#1783=B_SPLINE_CURVE_WITH_KNOTS('',3,(#168679,#168680,#168681,#168682,#168683,
#168684,#168685,#168686,#168687,#168688,#168689,#168690,#168691,#168692,
#168693,#168694,#168695,#168696,#168697,#168698,#168699,#168700,#168701,
#168702,#168703,#168704,#168705,#168706,#168707,#168708,#168709,#168710,
#168711,#168712,#168713,#168714,#168715,#168716,#168717,#168718,#168719,
#168720,#168721,#168722,#168723,#168724,#168725,#168726,#168727,#168728,
#168729,#168730,#168731,#168732,#168733,#168734,#168735,#168736,#168737,
#168738,#168739,#168740,#168741,#168742,#168743,#168744,#168745,#168746,
#168747,#168748,#168749,#168750,#168751,#168752,#168753,#168754,#168755,
#168756,#168757,#168758,#168759,#168760,#168761,#168762,#168763,#168764,
#168765,#168766,#168767,#168768,#168769,#168770,#168771,#168772,#168773,
#168774,#168775,#168776,#168777,#168778,#168779,#168780,#168781,#168782,
#168783,#168784,#168785,#168786,#168787,#168788,#168789,#168790,#168791,
#168792,#168793,#168794,#168795,#168796,#168797,#168798,#168799,#168800,
#168801,#168802,#168803,#168804,#168805,#168806,#168807,#168808,#168809,
#168810,#168811,#168812,#168813,#168814,#168815,#168816,#168817,#168818,
#168819,#168820,#168821,#168822,#168823,#168824,#168825,#168826,#168827,
#168828,#168829,#168830,#168831,#168832,#168833,#168834,#168835,#168836,
#168837,#168838,#168839,#168840,#168841,#168842,#168843,#168844,#168845,
#168846,#168847,#168848,#168849,#168850,#168851,#168852,#168853,#168854,
#168855,#168856,#168857,#168858,#168859,#168860,#168861,#168862,#168863,
#168864,#168865,#168866,#168867,#168868,#168869,#168870,#168871,#168872,
#168873,#168874,#168875,#168876,#168877,#168878,#168879,#168880,#168881,
#168882,#168883,#168884,#168885,#168886,#168887,#168888,#168889,#168890,
#168891,#168892,#168893,#168894,#168895,#168896,#168897,#168898,#168899,
#168900,#168901,#168902,#168903,#168904),.UNSPECIFIED.,.F.,.F.,(4,2,2,2,
2,2,2,2,2,2,2,2,2,2,2,2,2,2,2,2,2,2,2,2,2,2,2,2,2,2,2,2,2,2,2,2,2,2,2,2,
2,2,2,2,2,2,2,2,2,2,2,2,2,2,2,2,2,2,2,2,2,2,2,2,2,2,2,2,2,2,2,2,2,2,2,2,
2,2,2,2,2,2,2,2,2,2,2,2,2,2,2,2,2,2,2,2,2,2,2,2,2,2,2,2,2,2,2,2,2,2,2,2,
4),(0.000629332229582586,0.0482573633288315,0.0568193170551446,0.0589064612736026,
0.0601221095219334,0.0611992138773799,0.062584716532025,0.0648776103157659,
0.0786443976343827,0.120752779311643,0.14613932269728,0.159987626849096,
0.163516551337431,0.165693677576201,0.167609091198328,0.169994401368663,
0.173679853376456,0.191581938916001,0.198098502048847,0.242174718696393,
0.267696256798199,0.270413011096965,0.271762538844294,0.272833962575786,
0.274088923348135,0.276294079630585,0.285361610131089,0.288512788438226,
0.292119880904416,0.299321262310599,0.344360823284317,0.361848219246277,
0.372572793949327,0.375868084933978,0.377951621868027,0.379888330021888,
0.382404997095814,0.386615880088181,0.417193768036229,0.447298528592423,
0.470014542107235,0.480465934499665,0.482686756419762,0.48393186660931,
0.485004267210109,0.486367114909076,0.488535210969449,0.499945914043641,
0.504034520254718,0.504274790767321,0.511101106317111,0.524851430062145,
0.557709293246772,0.574269799213613,0.584580239844121,0.587828872151129,
0.589902177540771,0.591842863955748,0.594384079573048,0.59867925978644,
0.633800476137799,0.68271983574467,0.692502772744039,0.694679846759915,
0.695915445100066,0.696989200845538,0.698366225332436,0.700580854735983,
0.712810635935287,0.762460585500933,0.791343503503508,0.797798556630073,
0.800510952929573,0.802473412959469,0.804265417018526,0.807126526334425,
0.813986937857747,0.867411151635365,0.89311122459648,0.904365135933374,
0.906634695762748,0.907890533747698,0.908962013437402,0.910310722116163,
0.912936588292257,0.929095934771815,0.929561755882191,0.973907069665223,
1.00327706802672,1.00978979739154,1.01251194992555,1.01447626492199,1.0162664021171,
1.01911683260179,1.0259121107722,1.0801223800764,1.1052865151388,1.11640193197941,
1.11866349939461,1.11991763664288,1.12098932616527,1.12234041909693,1.12497719842511,
1.14140829716088,1.19199685838209,1.20970840693508,1.22053206228131,1.22383857175399,
1.22592477151939,1.22786090190283,1.23037249208948,1.23456537884827,1.25962401162403),
 .UNSPECIFIED.);
#1784=B_SPLINE_CURVE_WITH_KNOTS('',3,(#168906,#168907,#168908,#168909,#168910,
#168911,#168912,#168913,#168914,#168915,#168916,#168917,#168918,#168919,
#168920,#168921,#168922,#168923,#168924,#168925,#168926,#168927,#168928,
#168929,#168930,#168931,#168932,#168933,#168934,#168935,#168936,#168937,
#168938,#168939,#168940,#168941,#168942,#168943,#168944,#168945,#168946,
#168947,#168948,#168949,#168950,#168951,#168952,#168953,#168954,#168955,
#168956,#168957,#168958,#168959,#168960,#168961,#168962,#168963,#168964,
#168965,#168966,#168967,#168968,#168969,#168970,#168971,#168972,#168973,
#168974,#168975,#168976,#168977,#168978,#168979,#168980,#168981,#168982,
#168983,#168984,#168985,#168986,#168987,#168988,#168989,#168990,#168991,
#168992,#168993,#168994,#168995,#168996,#168997,#168998,#168999,#169000,
#169001,#169002,#169003,#169004,#169005,#169006,#169007,#169008,#169009,
#169010,#169011,#169012,#169013,#169014,#169015,#169016,#169017,#169018,
#169019,#169020,#169021,#169022,#169023,#169024,#169025,#169026,#169027,
#169028,#169029,#169030,#169031,#169032,#169033,#169034,#169035,#169036,
#169037,#169038,#169039,#169040,#169041,#169042,#169043,#169044,#169045,
#169046,#169047,#169048,#169049,#169050,#169051,#169052,#169053,#169054,
#169055,#169056,#169057,#169058,#169059,#169060,#169061,#169062,#169063,
#169064,#169065,#169066,#169067,#169068,#169069,#169070,#169071,#169072,
#169073,#169074,#169075,#169076,#169077,#169078,#169079,#169080,#169081,
#169082,#169083,#169084,#169085,#169086,#169087,#169088,#169089,#169090,
#169091,#169092,#169093,#169094,#169095,#169096,#169097,#169098,#169099,
#169100,#169101,#169102,#169103,#169104,#169105,#169106,#169107,#169108,
#169109,#169110,#169111,#169112,#169113,#169114,#169115,#169116,#169117,
#169118,#169119,#169120,#169121,#169122,#169123,#169124,#169125),
 .UNSPECIFIED.,.F.,.F.,(4,2,2,2,2,2,2,2,2,2,2,2,2,2,2,2,2,2,2,2,2,2,2,2,
2,2,2,2,2,2,2,2,2,2,2,2,2,2,2,2,2,2,2,2,2,2,2,2,2,2,2,2,2,2,2,2,2,2,2,2,
2,2,2,2,2,2,2,2,2,2,2,2,2,2,2,2,2,2,2,2,2,2,2,2,2,2,2,2,2,2,2,2,2,2,2,2,
2,2,2,2,2,2,2,2,2,2,2,2,2,4),(1.40839008782515,1.42691295402479,1.46582634767065,
1.47396801211054,1.491240619284,1.49390897104638,1.49526669837756,1.49633871234769,
1.49758756100695,1.49982541509922,1.51055030637073,1.53425079338281,1.56162148035616,
1.59355075685834,1.59778999759066,1.60031497971922,1.60225305038923,1.60433311502111,
1.60761245417449,1.61819321096669,1.6353583907911,1.68108903783519,1.68786757938709,
1.70330445862708,1.70567189461123,1.70707928880048,1.70815936140263,1.70936279676019,
1.7113947314429,1.71928758134134,1.73401038903081,1.76304115779599,1.80542080777784,
1.80971357198255,1.81225412704556,1.81419474103193,1.81626838716067,1.81951842550255,
1.8298406023543,1.84642919553635,1.87933877755081,1.89535760794404,1.89906704082739,
1.91519272937833,1.91782051739067,1.91916955752039,1.92024095617011,1.92149630652645,
1.92376397963471,1.93498869485887,1.96057453365421,2.01411249530492,2.02095981388174,
2.02381858724575,2.02561003931624,2.02757263529074,2.03028657357222,2.03675173263053,
2.09085791764579,2.12691082377215,2.12977136490755,2.13114950752416,2.1322233166408,
2.13345806132456,2.13563143076813,2.14536175323461,2.19429673867642,2.22943289517577,
2.23371909577794,2.23625769081201,2.2381979174631,2.24027222715142,2.24352555853709,
2.25387725649414,2.2705314948256,2.30349473002634,2.32242311388581,2.32484986247365,
2.33931586075786,2.34164253155749,2.34303795371653,2.34411632436838,2.34532621080509,
2.34738741397025,2.35562855478718,2.37132356966962,2.41418052996645,2.44164464922037,
2.44613896165899,2.44853219799288,2.45039850434395,2.45250822153758,2.45472513303732,
2.45802319933091,2.50312882243945,2.54811753459776,2.5528410366246,2.55458266001092,
2.55560824090958,2.55670048669667,2.55821035269146,2.56179035326915,2.59939070000387,
2.64830575180194,2.65646873999949,2.65954002493247,2.6613713531806,2.66321533633006,
2.66550720848957,2.66757157114197),.UNSPECIFIED.);
#1785=B_SPLINE_CURVE_WITH_KNOTS('',3,(#169126,#169127,#169128,#169129,#169130,
#169131,#169132,#169133,#169134,#169135),.UNSPECIFIED.,.F.,.F.,(4,2,2,2,
4),(0.000823830745865882,0.00400944464107275,0.0104637662401864,0.0609495485411902,
0.0751148559371182),.UNSPECIFIED.);
#1786=B_SPLINE_CURVE_WITH_KNOTS('',3,(#169141,#169142,#169143,#169144,#169145,
#169146),.UNSPECIFIED.,.F.,.F.,(4,2,4),(2.59315594695257,2.608916316382,
2.66742168368829),.UNSPECIFIED.);
#1787=B_SPLINE_CURVE_WITH_KNOTS('',3,(#169147,#169148,#169149,#169150,#169151,
#169152,#169153,#169154,#169155,#169156),.UNSPECIFIED.,.F.,.F.,(4,1,1,1,
1,1,1,4),(152.455231433536,152.821976844167,153.820813294129,154.819649744091,
155.818486194052,156.817322644014,157.816159093976,158.388969095546),
 .UNSPECIFIED.);
#1788=B_SPLINE_CURVE_WITH_KNOTS('',3,(#169157,#169158,#169159,#169160,#169161,
#169162,#169163,#169164,#169165,#169166,#169167,#169168,#169169,#169170,
#169171,#169172,#169173,#169174,#169175,#169176,#169177,#169178,#169179,
#169180,#169181,#169182,#169183,#169184,#169185,#169186,#169187,#169188,
#169189,#169190,#169191,#169192,#169193,#169194,#169195,#169196,#169197,
#169198,#169199,#169200,#169201,#169202,#169203,#169204,#169205,#169206,
#169207,#169208,#169209,#169210,#169211,#169212,#169213,#169214,#169215,
#169216,#169217,#169218,#169219,#169220,#169221,#169222,#169223,#169224,
#169225,#169226,#169227,#169228,#169229,#169230,#169231,#169232,#169233,
#169234,#169235,#169236,#169237,#169238,#169239,#169240,#169241,#169242,
#169243,#169244,#169245,#169246,#169247,#169248,#169249,#169250,#169251,
#169252,#169253,#169254,#169255,#169256,#169257,#169258,#169259,#169260,
#169261,#169262,#169263,#169264,#169265,#169266,#169267,#169268,#169269,
#169270,#169271,#169272,#169273,#169274,#169275,#169276,#169277,#169278,
#169279,#169280,#169281,#169282,#169283,#169284,#169285,#169286,#169287,
#169288,#169289,#169290,#169291,#169292,#169293,#169294,#169295,#169296,
#169297,#169298,#169299,#169300,#169301,#169302,#169303,#169304,#169305,
#169306,#169307,#169308,#169309,#169310,#169311,#169312,#169313,#169314,
#169315,#169316,#169317,#169318,#169319,#169320,#169321,#169322,#169323,
#169324,#169325,#169326,#169327,#169328,#169329,#169330,#169331,#169332,
#169333,#169334,#169335,#169336,#169337,#169338,#169339,#169340,#169341,
#169342,#169343,#169344,#169345,#169346,#169347,#169348,#169349,#169350,
#169351,#169352,#169353,#169354,#169355,#169356,#169357,#169358,#169359,
#169360,#169361,#169362,#169363,#169364,#169365,#169366,#169367,#169368,
#169369,#169370,#169371,#169372,#169373,#169374,#169375,#169376,#169377,
#169378,#169379,#169380,#169381,#169382,#169383,#169384,#169385,#169386,
#169387,#169388,#169389,#169390,#169391,#169392,#169393,#169394,#169395,
#169396,#169397,#169398,#169399,#169400,#169401,#169402,#169403,#169404,
#169405,#169406,#169407,#169408,#169409,#169410,#169411,#169412,#169413,
#169414,#169415,#169416,#169417,#169418,#169419,#169420,#169421,#169422,
#169423,#169424,#169425,#169426,#169427,#169428,#169429,#169430,#169431,
#169432,#169433,#169434),.UNSPECIFIED.,.F.,.F.,(4,2,2,2,2,2,2,2,2,2,2,2,
2,2,2,2,2,2,2,2,2,2,2,2,2,2,2,2,2,2,2,2,2,2,2,2,2,2,2,2,2,2,2,2,2,2,2,2,
2,2,2,2,2,2,2,2,2,2,2,2,2,2,2,2,2,2,2,2,2,2,2,2,2,2,2,2,2,2,2,2,2,2,2,2,
2,2,2,2,2,2,2,2,2,2,2,2,2,2,2,2,2,2,2,2,2,2,2,2,2,2,2,2,2,2,2,2,2,2,2,2,
2,2,2,2,2,2,2,2,2,2,2,2,2,2,2,2,2,2,4),(0.0751148559371182,0.0860173565209092,
0.0971067048898559,0.099366421733957,0.100620005721105,0.101691511545057,
0.103042742115049,0.105680884786454,0.122156785029108,0.172105730457344,
0.19018988390567,0.201175650792015,0.203636608709365,0.20592175810014,0.205936339486492,
0.205951514815512,0.205967323561641,0.205983808940996,0.206001018358443,
0.206019003919534,0.206037823133189,0.206057539636935,0.206078224011931,
0.206099954803837,0.206122819810584,0.206146917423792,0.206172358373818,
0.206199267857957,0.20622778807395,0.206258081290851,0.206290333750001,
0.206324760463609,0.20636161164916,0.206401180049667,0.206443809270907,
0.208321243029849,0.210755231903719,0.21543366746984,0.25055489342284,0.299497528275576,
0.309248234611211,0.311423000670789,0.312658039605414,0.313731789764809,
0.315109435347169,0.317967508302371,0.354058597180914,0.386748527096364,
0.409232518987205,0.414876188662865,0.41744565234437,0.419383843388974,
0.421211117362214,0.423755154818648,0.430409589924325,0.486119084923605,
0.510275166526602,0.521123209584095,0.523368751289448,0.524619354116576,
0.525691314061793,0.527046964930249,0.529191138841733,0.540205037851785,
0.591483586306157,0.620132182606221,0.626559385061205,0.629267098770382,
0.631228718645903,0.63302170791922,0.635888200213497,0.642781266181648,
0.695789031150177,0.72177847968669,0.733106392775542,0.735380227068554,
0.736636999189641,0.737708406864187,0.739055918696434,0.741676199297979,
0.757693834792938,0.763001774591121,0.774891703142893,0.777783592845092,
0.810579437265844,0.833225470791656,0.838891373722051,0.841465103814933,
0.843404133354895,0.845230450360933,0.847770352469685,0.854397290928634,
0.91039599306278,0.934368765256254,0.945167857462076,0.947410618365238,
0.948660704734029,0.949732858662897,0.951089571798029,0.953236957396969,
0.964299921129829,1.01544515888258,1.04417038111282,1.05060707288519,1.05331658161546,
1.05527870280231,1.05707160072483,1.05993675177385,1.06682040084819,1.11996764026672,
1.14586756475152,1.15717322464207,1.15944597457333,1.16070260234554,1.16177416341594,
1.16312222008114,1.16574459494106,1.18179282283111,1.185904715611,1.20159687313965,
1.23448609797719,1.25727490290768,1.26296037265423,1.2655378736431,1.2674776709501,
1.26930319149391,1.27183955315164,1.27844296751682,1.33468292779439,1.35363648187875,
1.36863946196255,1.37098961041877,1.3723921633433,1.37347181593448,1.37467844110652,
1.37672375260365,1.38476866900953,1.39990963280193,1.40880224667499),
 .UNSPECIFIED.);
#1789=B_SPLINE_CURVE_WITH_KNOTS('',3,(#169439,#169440,#169441,#169442,#169443,
#169444,#169445,#169446,#169447,#169448,#169449,#169450,#169451,#169452,
#169453,#169454,#169455,#169456,#169457,#169458,#169459,#169460,#169461,
#169462,#169463,#169464,#169465,#169466,#169467,#169468,#169469,#169470,
#169471,#169472,#169473,#169474,#169475,#169476,#169477,#169478,#169479,
#169480,#169481,#169482,#169483,#169484,#169485,#169486,#169487,#169488,
#169489,#169490,#169491,#169492,#169493,#169494,#169495,#169496,#169497,
#169498,#169499,#169500,#169501,#169502,#169503,#169504,#169505,#169506,
#169507,#169508,#169509,#169510,#169511,#169512,#169513,#169514,#169515,
#169516,#169517,#169518,#169519,#169520,#169521,#169522,#169523,#169524,
#169525,#169526,#169527,#169528,#169529,#169530,#169531,#169532,#169533,
#169534,#169535,#169536,#169537,#169538,#169539,#169540,#169541,#169542,
#169543,#169544,#169545,#169546,#169547,#169548,#169549,#169550,#169551,
#169552,#169553,#169554,#169555,#169556,#169557,#169558,#169559,#169560,
#169561,#169562,#169563,#169564,#169565,#169566,#169567,#169568,#169569,
#169570,#169571,#169572,#169573,#169574,#169575,#169576,#169577,#169578,
#169579,#169580,#169581,#169582,#169583,#169584,#169585,#169586,#169587,
#169588,#169589,#169590,#169591,#169592,#169593,#169594,#169595,#169596,
#169597,#169598,#169599,#169600,#169601,#169602,#169603,#169604,#169605,
#169606,#169607,#169608,#169609,#169610,#169611,#169612,#169613,#169614,
#169615,#169616,#169617,#169618,#169619,#169620,#169621,#169622,#169623,
#169624,#169625,#169626,#169627,#169628,#169629,#169630,#169631,#169632,
#169633,#169634,#169635,#169636,#169637,#169638,#169639,#169640,#169641,
#169642,#169643,#169644,#169645,#169646,#169647,#169648,#169649,#169650,
#169651,#169652,#169653,#169654,#169655,#169656,#169657,#169658,#169659,
#169660,#169661,#169662,#169663,#169664,#169665,#169666,#169667,#169668,
#169669,#169670,#169671,#169672),.UNSPECIFIED.,.F.,.F.,(4,2,2,2,2,2,2,2,
2,2,2,2,2,2,2,2,2,2,2,2,2,2,2,2,2,2,2,2,2,2,2,2,2,2,2,2,2,2,2,2,2,2,2,2,
2,2,2,2,2,2,2,2,2,2,2,2,2,2,2,2,2,2,2,2,2,2,2,2,2,2,2,2,2,2,2,2,2,2,2,2,
2,2,2,2,2,2,2,2,2,2,2,2,2,2,2,2,2,2,2,2,2,2,2,2,2,2,2,2,2,2,2,2,2,2,2,2,
4),(1.2596092693515,1.26784056841611,1.2907030567374,1.30119586166856,1.30341928440153,
1.30466495350844,1.3057372346681,1.30709916325351,1.30978754790108,1.32763512290863,
1.33373204541121,1.37574265376523,1.40292854542174,1.40705404731663,1.40954560736123,
1.41147833458491,1.4135728603315,1.41691845362249,1.42810815351804,1.44666701723586,
1.49069798611586,1.49656822344423,1.51244823745516,1.51506158391389,1.51640744634026,
1.5174786193471,1.51873640232671,1.52101503445713,1.53242869128707,1.55875522997995,
1.61123422843723,1.61816336233886,1.621035778792,1.62282984253785,1.62479053416427,
1.62749310976847,1.63388991324282,1.6817978741314,1.72137455636647,1.72610765750908,
1.72785087451443,1.72887686118778,1.72996902526844,1.73147803536465,1.73505268959622,
1.77422753331241,1.82298231529457,1.83011261701673,1.8330184057441,1.8348185296299,
1.83677412553914,1.8394484687519,1.84568047266152,1.87272244748268,1.9134469125147,
1.93614300379738,1.93899644014806,1.94037318987295,1.94144686727011,1.94268253522423,
1.94486010182034,1.9546517296156,2.00353502824768,2.03864077367805,2.04293545726612,
2.04547651510881,2.04741714815061,2.04949046049159,2.05273923559215,2.06305114794245,
2.07961726688403,2.11250761211196,2.12707470125624,2.13238357672141,2.1484237410175,
2.15104509852067,2.15239272196825,2.15346399410987,2.15472035750734,2.1569927688334,
2.16830014810116,2.19420894063555,2.24727819003548,2.25416222114205,2.25702700600421,
2.2588195257827,2.26078111927962,2.26348968281929,2.26992308807602,2.29863084376951,
2.34984288103329,2.36088073530258,2.36302629524007,2.36438230460374,2.36545420270438,
2.36670434047412,2.36894807597475,2.37976923032601,2.40382441604716,2.45963858842994,
2.46627634892691,2.468817626103,2.47064406087855,2.47252013026213,2.47500439199581,
2.47774260579395,2.48229452037214,2.49162589168426,2.54226133630486,2.57203625244806,
2.57495062302803,2.57633923563372,2.57741405840187,2.57864197125914,2.5807844665034,
2.59007764170921,2.59315594695257),.UNSPECIFIED.);
#1790=B_SPLINE_CURVE_WITH_KNOTS('',3,(#169674,#169675,#169676,#169677,#169678,
#169679,#169680,#169681,#169682,#169683,#169684,#169685,#169686,#169687,
#169688,#169689,#169690,#169691,#169692,#169693,#169694,#169695,#169696,
#169697,#169698,#169699,#169700,#169701,#169702,#169703,#169704,#169705,
#169706,#169707,#169708,#169709,#169710,#169711,#169712,#169713,#169714,
#169715,#169716,#169717,#169718,#169719,#169720,#169721,#169722,#169723,
#169724,#169725,#169726,#169727,#169728,#169729,#169730,#169731,#169732,
#169733,#169734,#169735,#169736,#169737,#169738,#169739,#169740,#169741,
#169742,#169743,#169744,#169745,#169746,#169747,#169748,#169749,#169750,
#169751,#169752,#169753,#169754,#169755,#169756,#169757,#169758,#169759,
#169760,#169761,#169762,#169763,#169764,#169765,#169766,#169767,#169768,
#169769,#169770,#169771,#169772,#169773,#169774,#169775,#169776,#169777,
#169778,#169779,#169780,#169781,#169782,#169783,#169784,#169785,#169786,
#169787,#169788,#169789,#169790,#169791,#169792,#169793,#169794,#169795,
#169796,#169797,#169798,#169799,#169800,#169801,#169802,#169803,#169804,
#169805,#169806,#169807,#169808,#169809,#169810,#169811,#169812,#169813,
#169814,#169815,#169816,#169817,#169818,#169819,#169820,#169821,#169822,
#169823,#169824,#169825,#169826,#169827,#169828,#169829,#169830,#169831,
#169832,#169833,#169834,#169835,#169836,#169837,#169838,#169839,#169840,
#169841,#169842,#169843,#169844,#169845,#169846,#169847,#169848,#169849,
#169850,#169851,#169852,#169853,#169854,#169855,#169856,#169857,#169858,
#169859,#169860,#169861,#169862,#169863,#169864,#169865,#169866,#169867,
#169868,#169869,#169870,#169871,#169872,#169873,#169874,#169875,#169876,
#169877,#169878,#169879,#169880,#169881,#169882,#169883,#169884,#169885,
#169886,#169887,#169888,#169889,#169890,#169891,#169892,#169893,#169894,
#169895,#169896,#169897,#169898,#169899),.UNSPECIFIED.,.F.,.F.,(4,2,2,2,
2,2,2,2,2,2,2,2,2,2,2,2,2,2,2,2,2,2,2,2,2,2,2,2,2,2,2,2,2,2,2,2,2,2,2,2,
2,2,2,2,2,2,2,2,2,2,2,2,2,2,2,2,2,2,2,2,2,2,2,2,2,2,2,2,2,2,2,2,2,2,2,2,
2,2,2,2,2,2,2,2,2,2,2,2,2,2,2,2,2,2,2,2,2,2,2,2,2,2,2,2,2,2,2,2,2,2,2,2,
4),(1.40880224667499,1.43961157073764,1.47086924577839,1.47509586135457,
1.47761755273777,1.4795555625412,1.48163797986083,1.48492615019491,1.49558026185905,
1.51290857721919,1.55319610960695,1.58019008650297,1.58309251547741,1.58447908464852,
1.58555400903655,1.58678392347576,1.5889343406719,1.59833078069535,1.64757023363411,
1.68278989810848,1.68708716824877,1.6896293560631,1.69157062179235,1.69364438702036,
1.69689340654677,1.70720218269439,1.72375957064368,1.75664804549484,1.77020265705881,
1.77751739841314,1.78186853654147,1.79304041252785,1.79519457097785,1.79655336872559,
1.79762571522802,1.79887436353224,1.8011103953453,1.8117989510688,1.835362518185,
1.89195134346187,1.89851313365991,1.90104272958297,1.90286637716281,1.90480695521465,
1.90739022680765,1.91310790195329,1.93614073437515,1.96921271377465,1.99068775996686,
2.0047808629009,2.0070899754305,2.00848038597147,2.00955828336901,2.01077144685872,
2.01284673118582,2.02125710714381,2.03743457119017,2.07973706793973,2.10709479977152,
2.11122544366403,2.11371882707531,2.1156522100081,2.11774669010319,2.12109057481832,
2.13225934821722,2.15076801969815,2.19595391381947,2.21639908458475,2.21919539700334,
2.22056098506142,2.22163380413166,2.22287742419837,2.22509073036959,2.23541950216045,
2.2576968117535,2.31632919780073,2.322643564461,2.32513223497133,2.32694511889544,
2.32889183966653,2.33151389671942,2.33744727820757,2.36212117128085,2.39106278201487,
2.42837343754691,2.43120665730518,2.43257948888165,2.43365287752092,2.43486646680045,
2.43697180760491,2.43957284873205,2.44499399831273,2.46045951398037,2.50169974687982,
2.53100449050529,2.53519459596823,2.53770535330162,2.53964132024482,2.54172781584236,
2.54503580178152,2.55587324477922,2.5736188983316,2.61954524127795,2.62787682755203,
2.64088199695592,2.64313751906312,2.64452688409231,2.64560190538519,2.64661071036363,
2.64782386588663,2.64961025778248,2.65534542984729,2.66801380144248),
 .UNSPECIFIED.);
#1791=B_SPLINE_CURVE_WITH_KNOTS('',3,(#169900,#169901,#169902,#169903,#169904,
#169905,#169906,#169907,#169908,#169909,#169910,#169911,#169912),
 .UNSPECIFIED.,.F.,.F.,(4,3,3,3,4),(-161.271232439372,-161.169466228941,
-161.067655520383,-160.965694042516,-160.920671713183),.UNSPECIFIED.);
#1792=B_SPLINE_CURVE_WITH_KNOTS('',3,(#169918,#169919,#169920,#169921,#169922,
#169923,#169924,#169925,#169926,#169927,#169928,#169929,#169930),
 .UNSPECIFIED.,.F.,.F.,(4,3,3,3,4),(170.955339710339,171.057208849126,171.158971104986,
171.260660144695,171.305836655045),.UNSPECIFIED.);
#1793=B_SPLINE_CURVE_WITH_KNOTS('',3,(#169931,#169932,#169933,#169934,#169935,
#169936,#169937,#169938,#169939,#169940,#169941,#169942,#169943,#169944,
#169945,#169946,#169947,#169948,#169949,#169950,#169951,#169952,#169953,
#169954,#169955,#169956,#169957,#169958,#169959,#169960,#169961,#169962,
#169963,#169964,#169965,#169966,#169967,#169968,#169969,#169970,#169971,
#169972,#169973,#169974,#169975,#169976,#169977,#169978,#169979,#169980,
#169981,#169982,#169983,#169984,#169985,#169986,#169987,#169988,#169989,
#169990,#169991,#169992,#169993,#169994,#169995,#169996,#169997,#169998,
#169999,#170000,#170001,#170002,#170003,#170004,#170005,#170006,#170007,
#170008,#170009,#170010,#170011,#170012,#170013,#170014,#170015,#170016,
#170017,#170018,#170019,#170020,#170021,#170022,#170023,#170024,#170025,
#170026,#170027,#170028,#170029,#170030,#170031,#170032,#170033,#170034,
#170035,#170036,#170037,#170038,#170039,#170040,#170041,#170042,#170043,
#170044,#170045,#170046,#170047,#170048,#170049,#170050,#170051,#170052,
#170053,#170054,#170055,#170056,#170057,#170058,#170059,#170060,#170061,
#170062,#170063,#170064,#170065,#170066,#170067,#170068,#170069,#170070,
#170071,#170072,#170073,#170074,#170075,#170076,#170077,#170078,#170079,
#170080,#170081,#170082,#170083,#170084,#170085,#170086,#170087,#170088,
#170089,#170090,#170091,#170092,#170093,#170094,#170095,#170096,#170097,
#170098,#170099,#170100,#170101,#170102,#170103,#170104,#170105,#170106,
#170107,#170108,#170109,#170110,#170111,#170112,#170113,#170114,#170115,
#170116,#170117,#170118,#170119,#170120,#170121,#170122,#170123,#170124,
#170125,#170126,#170127,#170128,#170129,#170130,#170131,#170132,#170133,
#170134,#170135,#170136,#170137,#170138,#170139,#170140,#170141,#170142,
#170143,#170144,#170145,#170146,#170147,#170148,#170149,#170150,#170151,
#170152),.UNSPECIFIED.,.F.,.F.,(4,2,2,2,2,2,2,2,2,2,2,2,2,2,2,2,2,2,2,2,
2,2,2,2,2,2,2,2,2,2,2,2,2,2,2,2,2,2,2,2,2,2,2,2,2,2,2,2,2,2,2,2,2,2,2,2,
2,2,2,2,2,2,2,2,2,2,2,2,2,2,2,2,2,2,2,2,2,2,2,2,2,2,2,2,2,2,2,2,2,2,2,2,
2,2,2,2,2,2,2,2,2,2,2,2,2,2,2,2,2,2,4),(0.000655565290617039,0.0215326227087458,
0.0285520710486535,0.0303960629521583,0.0316335607159248,0.0326484285716836,
0.0337175069904086,0.0350633930395249,0.0377854288917679,0.0559544034455085,
0.0616383873005818,0.0739383147691349,0.0845186242864435,0.106384758506318,
0.122977226240448,0.133286131125452,0.136520278985314,0.13858070980606,
0.140506707952375,0.143024766653336,0.147271569276199,0.192337973141826,
0.22091807838469,0.234451255841387,0.241869173568767,0.243841554482253,
0.244851270225045,0.245918308402917,0.247244927128634,0.249294265923087,
0.258883353206475,0.318505182680996,0.335297146712612,0.345718998927197,
0.348985053123623,0.351065350606082,0.353009727700483,0.35555172346558,
0.359839415602083,0.39423194403244,0.443433223563238,0.453286877168867,
0.455474595401037,0.456715604686166,0.457791868669989,0.459170491607426,
0.462028184696963,0.484797499509343,0.527329548590344,0.545904458535281,
0.557102064951541,0.560449566794869,0.562545228055637,0.564478970452924,
0.566971800761908,0.571099347367187,0.598278955703666,0.640350658381965,
0.656908939161571,0.665449707380976,0.667534981446109,0.668750097521971,
0.66982654936366,0.6712113028048,0.67350376882571,0.687289260686422,0.698622940530256,
0.737950194812959,0.764492408746576,0.770660422150587,0.773322051898098,
0.775273872650231,0.777074388192578,0.77998939464479,0.787184938532417,
0.833860946690508,0.856214114887312,0.870037786566998,0.875062862512361,
0.878645356469889,0.880154645396697,0.881246079267879,0.882271364737024,
0.884011344247576,0.888723737535384,0.929075838788759,0.977359064926128,
0.982966799285399,0.985530056472904,0.987467732993937,0.989297600835379,
0.991850217201394,0.998557418009532,1.05366046053509,1.07817665918164,1.08912117441691,
1.09137327484703,1.09262569274372,1.09369779389037,1.09505198329242,1.09779132353903,
1.11614970257119,1.1651496610562,1.18898299999316,1.19480672140833,1.19740892751408,
1.19935221826704,1.20117007595888,1.20367843671327,1.21011170514138,1.2596092693515),
 .UNSPECIFIED.);
#1794=B_SPLINE_CURVE_WITH_KNOTS('',3,(#170154,#170155,#170156,#170157,#170158,
#170159,#170160,#170161,#170162,#170163,#170164,#170165,#170166,#170167,
#170168,#170169,#170170,#170171,#170172,#170173,#170174,#170175,#170176,
#170177,#170178,#170179,#170180,#170181,#170182,#170183,#170184,#170185,
#170186,#170187,#170188,#170189,#170190,#170191,#170192,#170193,#170194,
#170195,#170196,#170197,#170198,#170199,#170200,#170201,#170202,#170203,
#170204,#170205,#170206,#170207,#170208,#170209,#170210,#170211,#170212,
#170213,#170214,#170215,#170216,#170217,#170218,#170219,#170220,#170221,
#170222,#170223,#170224,#170225,#170226,#170227,#170228,#170229,#170230,
#170231,#170232,#170233,#170234,#170235,#170236,#170237,#170238,#170239,
#170240,#170241,#170242,#170243,#170244,#170245,#170246,#170247,#170248,
#170249,#170250,#170251,#170252,#170253,#170254,#170255,#170256,#170257,
#170258,#170259,#170260,#170261,#170262,#170263,#170264,#170265,#170266,
#170267,#170268,#170269,#170270,#170271,#170272,#170273,#170274,#170275,
#170276,#170277,#170278,#170279,#170280,#170281,#170282,#170283,#170284,
#170285,#170286,#170287,#170288,#170289,#170290,#170291,#170292,#170293,
#170294,#170295,#170296,#170297,#170298,#170299,#170300,#170301,#170302,
#170303,#170304,#170305,#170306,#170307,#170308,#170309,#170310,#170311,
#170312,#170313,#170314,#170315,#170316,#170317,#170318,#170319,#170320,
#170321,#170322,#170323,#170324,#170325,#170326,#170327,#170328,#170329,
#170330,#170331,#170332,#170333,#170334),.UNSPECIFIED.,.F.,.F.,(4,3,3,3,
3,3,3,3,3,3,3,3,3,3,3,3,3,3,3,3,3,3,3,3,3,3,3,3,3,3,3,3,3,3,3,3,3,3,3,3,
3,3,3,3,3,3,3,3,3,3,3,3,3,3,3,3,3,3,3,3,4),(-167.203857019737,-167.089811042057,
-166.975344485129,-166.860315113754,-166.805687143633,-166.702287417193,
-166.599041109048,-166.495916087595,-166.3928564475,-166.289828158908,-166.186797235114,
-166.083659421327,-165.980465294178,-165.877088339511,-165.806850693671,
-165.703453681301,-165.600210066751,-165.4970876947,-165.39403067537,-165.291004974943,
-165.187976602729,-165.084841265902,-164.981649577785,-164.878274973299,
-164.808014243709,-164.704622128712,-164.601383510577,-164.498266258922,
-164.395214433679,-164.292193993531,-164.189170940353,-164.08604097664,
-163.98285470024,-163.879485509913,-163.809177793747,-163.705782196268,
-163.602540045536,-163.499419203548,-163.396363754289,-163.293339661723,
-163.190312932971,-163.087179283398,-162.983989309662,-162.880616444552,
-162.810341343786,-162.706946383838,-162.603704872123,-162.500584668206,
-162.397529856099,-162.294506398816,-162.191480302535,-162.088347276647,
-161.985157922646,-161.881785663941,-161.811504893824,-161.709471729551,
-161.607582179598,-161.505807286823,-161.404097848661,-161.302405178504,
-161.271232439372),.UNSPECIFIED.);
#1795=B_SPLINE_CURVE_WITH_KNOTS('',3,(#170335,#170336,#170337,#170338,#170339,
#170340,#170341,#170342,#170343,#170344,#170345,#170346,#170347),
 .UNSPECIFIED.,.F.,.F.,(4,3,3,3,4),(-167.55333773927,-167.448855810974,
-167.344457556961,-167.240110620773,-167.203857020092),.UNSPECIFIED.);
#1796=B_SPLINE_CURVE_WITH_KNOTS('',3,(#170353,#170354,#170355,#170356,#170357,
#170358,#170359,#170360,#170361,#170362),.UNSPECIFIED.,.F.,.F.,(4,3,3,4),
(7.5925217235916,7.70650210579109,7.82442143144844,7.9423407571058),
 .UNSPECIFIED.);
#1797=B_SPLINE_CURVE_WITH_KNOTS('',3,(#170364,#170365,#170366,#170367,#170368,
#170369,#170370,#170371,#170372,#170373,#170374,#170375,#170376,#170377,
#170378,#170379,#170380,#170381,#170382,#170383,#170384,#170385,#170386,
#170387,#170388,#170389,#170390,#170391,#170392,#170393,#170394,#170395,
#170396,#170397,#170398,#170399,#170400,#170401,#170402,#170403,#170404,
#170405,#170406,#170407,#170408,#170409,#170410,#170411,#170412,#170413,
#170414,#170415,#170416,#170417,#170418,#170419,#170420,#170421,#170422,
#170423,#170424,#170425,#170426,#170427,#170428,#170429,#170430,#170431,
#170432,#170433,#170434,#170435,#170436,#170437,#170438,#170439,#170440,
#170441,#170442,#170443,#170444,#170445,#170446,#170447,#170448,#170449,
#170450,#170451,#170452,#170453,#170454,#170455,#170456,#170457,#170458,
#170459,#170460,#170461,#170462,#170463,#170464,#170465,#170466,#170467,
#170468,#170469,#170470,#170471,#170472,#170473,#170474,#170475,#170476,
#170477,#170478,#170479,#170480,#170481,#170482,#170483,#170484,#170485,
#170486,#170487,#170488,#170489,#170490,#170491,#170492,#170493,#170494,
#170495,#170496,#170497,#170498,#170499,#170500,#170501,#170502,#170503,
#170504,#170505,#170506,#170507,#170508,#170509,#170510,#170511,#170512,
#170513,#170514,#170515,#170516,#170517,#170518,#170519,#170520,#170521,
#170522,#170523,#170524,#170525,#170526,#170527,#170528,#170529,#170530,
#170531,#170532),.UNSPECIFIED.,.F.,.F.,(4,3,3,3,3,3,3,3,3,3,3,3,3,3,3,3,
3,3,3,3,3,3,3,3,3,3,3,3,3,3,3,3,3,3,3,3,3,3,3,3,3,3,3,3,3,3,3,3,3,3,3,3,
3,3,3,3,4),(2.00878451784277,2.1121038592252,2.21526978906708,2.31831430239281,
2.42129361283972,2.52424186610789,2.6271931648727,2.73024926544087,2.83336236205174,
2.93665172410156,2.99650934988563,3.10008230044164,3.20350555624697,3.30681221854451,
3.41005628885956,3.51327152250976,3.61649163431342,3.71982077793706,3.82320772460313,
3.92677776279761,3.99534579984751,4.09860814851247,4.20171513491831,4.30469859633612,
4.40761536822807,4.51049968437652,4.61338573414333,4.71637827780363,4.8194266839831,
4.92265880761429,4.99418224980938,5.09760357317466,5.20087154158791,5.30401821033476,
5.40709947808643,5.51014934245974,5.61320175788195,5.7163607823649,5.81957599567373,
5.92297359909413,5.99301869977126,6.09643423501025,6.19969678171233,6.30283860648641,
6.40591538895672,6.50896113435575,6.61200980509545,6.71516569207011,6.81837810297347,
6.92177347981602,6.99185514973314,7.09670699182257,7.20139082240131,7.30591390630536,
7.41034216218022,7.51471170479246,7.59252172323623),.UNSPECIFIED.);
#1798=B_SPLINE_CURVE_WITH_KNOTS('',3,(#170536,#170537,#170538,#170539,#170540,
#170541,#170542,#170543,#170544,#170545,#170546,#170547,#170548,#170549,
#170550,#170551,#170552,#170553,#170554,#170555,#170556,#170557,#170558,
#170559,#170560,#170561,#170562,#170563,#170564,#170565,#170566,#170567,
#170568,#170569,#170570,#170571,#170572,#170573,#170574,#170575,#170576,
#170577,#170578,#170579,#170580,#170581,#170582,#170583,#170584,#170585,
#170586,#170587,#170588,#170589,#170590,#170591,#170592,#170593,#170594,
#170595,#170596,#170597,#170598,#170599,#170600,#170601,#170602,#170603,
#170604,#170605,#170606,#170607,#170608,#170609,#170610,#170611,#170612,
#170613,#170614,#170615,#170616,#170617,#170618,#170619,#170620,#170621,
#170622,#170623,#170624,#170625,#170626,#170627,#170628,#170629,#170630,
#170631,#170632,#170633,#170634,#170635,#170636,#170637,#170638,#170639,
#170640,#170641,#170642,#170643,#170644,#170645,#170646,#170647,#170648,
#170649,#170650,#170651,#170652,#170653),.UNSPECIFIED.,.F.,.F.,(4,3,3,3,
3,3,3,3,3,3,3,3,3,3,3,3,3,3,3,3,3,3,3,3,3,3,3,3,3,3,3,3,3,3,3,3,3,3,3,4),
(-3.84103903298819,-3.73547282260037,-3.63371534129195,-3.532025649837,
-3.43036801686642,-3.32870675955683,-3.22694496839026,-3.12512265260723,
-3.0231391456354,-2.99650934988562,-2.89298804639364,-2.7896177431212,-2.6863657748023,
-2.58317744783227,-2.48001894053971,-2.37685647276339,-2.2735860348565,
-2.17025847843688,-2.06674831927575,-1.99767289992375,-1.89536969270601,
-1.79322053934975,-1.69118879043613,-1.58921974834484,-1.48727804733066,
-1.38532836211997,-1.28325632553546,-1.18112129116516,-1.0787805560955,
-0.998836449961877,-0.892562651586185,-0.780992320137912,-0.67507184468024,
-0.56925096547428,-0.463501942676278,-0.357797126152519,-0.25207917949123,
-0.14635615172218,-0.0405601678050039,0.),.UNSPECIFIED.);
#1799=B_SPLINE_CURVE_WITH_KNOTS('',3,(#170654,#170655,#170656,#170657,#170658,
#170659,#170660,#170661,#170662,#170663,#170664,#170665,#170666,#170667,
#170668,#170669,#170670,#170671,#170672,#170673,#170674,#170675,#170676,
#170677,#170678,#170679),.UNSPECIFIED.,.F.,.F.,(4,2,2,2,2,2,2,2,2,2,2,2,
4),(0.000655568373726633,0.0215326025103882,0.0285520600990642,0.030396058279881,
0.0316335578306403,0.032648424817314,0.0337175011697388,0.0350633794126454,
0.0377853822300375,0.0559534379118389,0.0616384583380826,0.0739384474895044,
0.0747573410445804),.UNSPECIFIED.);
#1800=B_SPLINE_CURVE_WITH_KNOTS('',3,(#170685,#170686,#170687,#170688,#170689,
#170690,#170691,#170692,#170693,#170694,#170695,#170696,#170697,#170698,
#170699,#170700,#170701,#170702,#170703,#170704,#170705,#170706,#170707,
#170708),.UNSPECIFIED.,.F.,.F.,(4,2,2,2,2,2,2,2,2,2,2,4),(2.59396097058535,
2.61966488148547,2.62799719025607,2.64100348253462,2.64325919998503,2.64464868542601,
2.64572379995559,2.64673269247101,2.64794595330706,2.64973250033605,2.6554681689063,
2.66813763591281),.UNSPECIFIED.);
#1801=B_SPLINE_CURVE_WITH_KNOTS('',3,(#170709,#170710,#170711,#170712,#170713,
#170714,#170715,#170716,#170717,#170718,#170719,#170720,#170721,#170722,
#170723,#170724,#170725,#170726,#170727,#170728,#170729,#170730,#170731,
#170732,#170733,#170734,#170735,#170736,#170737,#170738,#170739,#170740,
#170741,#170742,#170743,#170744,#170745,#170746,#170747,#170748,#170749,
#170750,#170751,#170752,#170753,#170754,#170755,#170756,#170757,#170758,
#170759,#170760,#170761,#170762,#170763,#170764,#170765,#170766,#170767,
#170768,#170769,#170770,#170771,#170772,#170773,#170774,#170775,#170776,
#170777,#170778,#170779,#170780,#170781,#170782,#170783,#170784,#170785,
#170786,#170787,#170788,#170789,#170790,#170791,#170792,#170793,#170794,
#170795,#170796,#170797,#170798,#170799,#170800,#170801,#170802,#170803,
#170804,#170805,#170806,#170807,#170808,#170809,#170810,#170811,#170812,
#170813,#170814,#170815,#170816,#170817,#170818,#170819,#170820,#170821,
#170822,#170823,#170824,#170825,#170826,#170827,#170828,#170829,#170830,
#170831,#170832,#170833,#170834,#170835,#170836,#170837,#170838,#170839,
#170840,#170841,#170842,#170843,#170844,#170845,#170846,#170847,#170848,
#170849,#170850,#170851,#170852,#170853,#170854,#170855,#170856,#170857,
#170858,#170859,#170860,#170861,#170862,#170863,#170864,#170865,#170866,
#170867,#170868,#170869,#170870,#170871,#170872,#170873,#170874,#170875,
#170876,#170877,#170878,#170879,#170880,#170881,#170882,#170883,#170884,
#170885,#170886,#170887,#170888,#170889),.UNSPECIFIED.,.F.,.F.,(4,3,3,3,
3,3,3,3,3,3,3,3,3,3,3,3,3,3,3,3,3,3,3,3,3,3,3,3,3,3,3,3,3,3,3,3,3,3,3,3,
3,3,3,3,3,3,3,3,3,3,3,3,3,3,3,3,3,3,3,3,4),(7.9423407571058,7.99069159969502,
8.0940913166079,8.19733761512875,8.30046262686177,8.40352225718067,8.50655053595679,
8.60958144990777,8.71271925388011,8.81591337121366,8.9192903161747,8.98952804965688,
9.09292506023253,9.19616867293108,9.29929104305031,9.40234806040229,9.50537375880478,
9.608402128953,9.71153746366316,9.81472914963136,9.91810375194011,9.98836449961875,
10.0917566187677,10.1949952411212,10.2981124970725,10.4011643266588,10.504184771191,
10.6072078287861,10.7103377969385,10.8135240777969,10.916893272565,10.9872009495806,
11.0905965451736,11.1938386939995,11.2969595340606,11.400014981379,11.5030390719965,
11.6060657987925,11.7091994464135,11.8123894181962,11.9157622813734,11.9860373995425,
12.0894323592964,12.1926738708075,12.2957940745085,12.3988488863923,12.5018723434439,
12.6048984394876,12.7080314651285,12.8112208188763,12.9145930773222,12.9848738495044,
13.0869196152918,13.1887917830724,13.2905669750553,13.3922809421219,13.493969350127,
13.5957283282564,13.697522003712,13.7994743430358,13.8757070301447),
 .UNSPECIFIED.);
#1802=B_SPLINE_CURVE_WITH_KNOTS('',3,(#170890,#170891,#170892,#170893,#170894,
#170895,#170896,#170897,#170898,#170899,#170900,#170901,#170902,#170903,
#170904,#170905,#170906,#170907,#170908,#170909,#170910,#170911,#170912,
#170913,#170914,#170915,#170916,#170917,#170918,#170919,#170920,#170921,
#170922,#170923,#170924,#170925,#170926,#170927,#170928,#170929,#170930,
#170931,#170932,#170933,#170934,#170935,#170936,#170937,#170938,#170939,
#170940,#170941,#170942,#170943,#170944,#170945,#170946,#170947,#170948,
#170949,#170950,#170951,#170952,#170953,#170954,#170955,#170956,#170957,
#170958,#170959,#170960,#170961,#170962,#170963,#170964,#170965,#170966,
#170967,#170968,#170969,#170970,#170971,#170972,#170973,#170974,#170975,
#170976,#170977,#170978,#170979,#170980,#170981,#170982,#170983,#170984,
#170985,#170986,#170987,#170988,#170989,#170990,#170991,#170992,#170993,
#170994,#170995,#170996,#170997,#170998,#170999,#171000,#171001,#171002,
#171003,#171004,#171005,#171006,#171007,#171008,#171009,#171010,#171011,
#171012,#171013,#171014,#171015,#171016,#171017,#171018,#171019,#171020,
#171021,#171022,#171023,#171024,#171025,#171026,#171027,#171028,#171029,
#171030,#171031,#171032,#171033,#171034,#171035,#171036,#171037,#171038,
#171039,#171040,#171041,#171042,#171043,#171044,#171045,#171046,#171047,
#171048,#171049,#171050,#171051,#171052,#171053,#171054,#171055,#171056,
#171057,#171058,#171059,#171060,#171061,#171062,#171063,#171064,#171065,
#171066,#171067,#171068,#171069,#171070,#171071,#171072,#171073,#171074,
#171075,#171076,#171077,#171078,#171079,#171080,#171081,#171082,#171083,
#171084,#171085,#171086,#171087,#171088,#171089,#171090,#171091,#171092,
#171093,#171094,#171095,#171096,#171097,#171098,#171099,#171100,#171101,
#171102,#171103,#171104,#171105,#171106,#171107,#171108,#171109,#171110,
#171111,#171112,#171113,#171114,#171115),.UNSPECIFIED.,.F.,.F.,(4,2,2,2,
2,2,2,2,2,2,2,2,2,2,2,2,2,2,2,2,2,2,2,2,2,2,2,2,2,2,2,2,2,2,2,2,2,2,2,2,
2,2,2,2,2,2,2,2,2,2,2,2,2,2,2,2,2,2,2,2,2,2,2,2,2,2,2,2,2,2,2,2,2,2,2,2,
2,2,2,2,2,2,2,2,2,2,2,2,2,2,2,2,2,2,2,2,2,2,2,2,2,2,2,2,2,2,2,2,2,2,2,2,
4),(0.0747573410445804,0.0845186705731368,0.106384833159163,0.122977268432354,
0.133286155948304,0.136520299082465,0.138580727010485,0.140506722518262,
0.143024777841391,0.147271574858557,0.192338078811951,0.220918211426313,
0.23445132756505,0.241869219920678,0.243841596800967,0.244851311040615,
0.245918348998624,0.247244968472377,0.249294309205372,0.258883419242254,
0.318505107182258,0.33529716797821,0.345719066135449,0.348985127201808,
0.351065427293654,0.353009805601841,0.355551801208321,0.359839489253536,
0.394231670214988,0.443432623867018,0.453286793494708,0.455474548716315,
0.456715567136985,0.457791830935739,0.459170443254487,0.462028080891041,
0.484795161151365,0.527329653025948,0.545904467624627,0.557102032473282,
0.560449529785833,0.562545189975799,0.564478932583876,0.566971764837944,
0.571099318266019,0.598279189460489,0.640351486123511,0.656909177905306,
0.665449744169385,0.667535001735122,0.668750113887454,0.669826566067397,
0.671211324852166,0.673503809869498,0.68728970579793,0.698623488257327,
0.737950319022652,0.76449243597379,0.77066043653915,0.773322063534953,0.775273883311026,
0.77707439868121,0.779989406474173,0.787184961628708,0.833860412060123,
0.856214203934402,0.870037822399162,0.875062884842747,0.878645371106983,
0.880154658430758,0.881246091825336,0.882271377615306,0.884011358682575,
0.88872376206493,0.929076069033313,0.977359083840166,0.982966816849575,
0.985530073990243,0.987467750712657,0.989297618920964,0.99185023608595,
0.998557440794016,1.05366042084994,1.07817664749199,1.08912117038505,1.09137327161863,
1.09262568986451,1.09369779112269,1.09505198049589,1.09779132050781,1.11614969127593,
1.16514965369926,1.18898299191255,1.19480671307616,1.19740891905937,1.19935220971603,
1.20117006731361,1.20367842793102,1.21011169596083,1.26784057161457,1.29070305801019,
1.30119586228216,1.30341928481243,1.30466495379317,1.30573723483708,1.30709916325547,
1.30978754749906,1.32763511612353,1.3337320454579,1.37574265902158,1.40292854662424,
1.4070540481674,1.40817976059961),.UNSPECIFIED.);
#1803=B_SPLINE_CURVE_WITH_KNOTS('',3,(#171120,#171121,#171122,#171123,#171124,
#171125,#171126,#171127,#171128,#171129,#171130,#171131,#171132,#171133,
#171134,#171135,#171136,#171137,#171138,#171139,#171140,#171141,#171142,
#171143,#171144,#171145,#171146,#171147,#171148,#171149,#171150,#171151,
#171152,#171153,#171154,#171155,#171156,#171157,#171158,#171159,#171160,
#171161,#171162,#171163,#171164,#171165,#171166,#171167,#171168,#171169,
#171170,#171171,#171172,#171173,#171174,#171175,#171176,#171177,#171178,
#171179,#171180,#171181,#171182,#171183,#171184,#171185,#171186,#171187,
#171188,#171189,#171190,#171191,#171192,#171193,#171194,#171195,#171196,
#171197,#171198,#171199,#171200,#171201,#171202,#171203,#171204,#171205,
#171206,#171207,#171208,#171209,#171210,#171211,#171212,#171213,#171214,
#171215,#171216,#171217,#171218,#171219,#171220,#171221,#171222,#171223,
#171224,#171225,#171226,#171227,#171228,#171229,#171230,#171231,#171232,
#171233,#171234,#171235,#171236,#171237,#171238,#171239,#171240,#171241,
#171242,#171243,#171244,#171245,#171246,#171247,#171248,#171249,#171250,
#171251,#171252,#171253,#171254,#171255,#171256,#171257,#171258,#171259,
#171260,#171261,#171262,#171263,#171264,#171265,#171266,#171267,#171268,
#171269,#171270,#171271,#171272,#171273,#171274,#171275,#171276,#171277,
#171278,#171279,#171280,#171281,#171282,#171283,#171284,#171285,#171286,
#171287,#171288,#171289,#171290,#171291,#171292,#171293,#171294,#171295,
#171296,#171297,#171298,#171299,#171300,#171301,#171302,#171303,#171304,
#171305,#171306,#171307,#171308,#171309,#171310,#171311,#171312,#171313,
#171314,#171315,#171316,#171317,#171318,#171319,#171320,#171321,#171322,
#171323,#171324,#171325,#171326,#171327,#171328,#171329,#171330,#171331,
#171332,#171333,#171334,#171335,#171336,#171337,#171338,#171339,#171340,
#171341,#171342,#171343,#171344,#171345,#171346,#171347,#171348,#171349,
#171350,#171351,#171352,#171353,#171354,#171355),.UNSPECIFIED.,.F.,.F.,
(4,2,2,2,2,2,2,2,2,2,2,2,2,2,2,2,2,2,2,2,2,2,2,2,2,2,2,2,2,2,2,2,2,2,2,
2,2,2,2,2,2,2,2,2,2,2,2,2,2,2,2,2,2,2,2,2,2,2,2,2,2,2,2,2,2,2,2,2,2,2,2,
2,2,2,2,2,2,2,2,2,2,2,2,2,2,2,2,2,2,2,2,2,2,2,2,2,2,2,2,2,2,2,2,2,2,2,2,
2,2,2,2,2,2,2,2,2,2,4),(1.26014274045541,1.26297209927859,1.26554984345313,
1.26748982372479,1.26931551641608,1.27185211719372,1.27845615377098,1.33470141050411,
1.35365674900082,1.36866114306478,1.37101151311199,1.37241419829855,1.37349395271473,
1.37470069170799,1.37674619619045,1.38479187235191,1.39993426723045,1.43963996922864,
1.47090055718122,1.47512757055363,1.47764949952585,1.47958769207543,1.48167030590745,
1.48495878685757,1.49561390783155,1.51294386781522,1.55323518103887,1.58023169425134,
1.58313439680814,1.58452109672224,1.58559612249024,1.58682615295961,1.58897677310651,
1.59837410128736,1.64761819587377,1.6828411695857,1.6871388447366,1.68968127223282,
1.6916227210389,1.69369668189028,1.69694600801346,1.70725575793492,1.72381471101445,
1.75670628863334,1.77026267743675,1.7775768382212,1.78191404428974,1.79310050992532,
1.79525569839796,1.7966148761427,1.79768734324328,1.79893592628009,1.8011713306124,
1.81184728693573,1.83536345053879,1.89203457860106,1.89858858463189,1.90111706860915,
1.90294053294031,1.90488148850446,1.90746624357967,1.91319125427484,1.93627703918399,
1.97002382608581,1.99225669543721,2.00498804876792,2.0072297005631,2.00861499200257,
2.00968972307797,2.0109203095309,2.01307400992551,2.02251793649443,2.07171202003201,
2.1069170963119,2.11121391611252,2.11375588398395,2.11569700849964,2.11777064877978,
2.12101952657924,2.13132830733565,2.14788613005514,2.18077366189977,2.21641126348564,
2.21927453521325,2.22065336931389,2.22172742429494,2.22296212080951,2.22513461690257,
2.23484807285045,2.28380809990575,2.31894137921001,2.32323714025563,2.32577875681878,
2.32771977142962,2.32979344784715,2.33304270287299,2.34335538374999,2.35992205251161,
2.39137460394602,2.42846956081233,2.43130759466556,2.43268144536678,2.43375500902394,
2.43496810604408,2.43707097282812,2.43966818532776,2.44507801256525,2.46049453097618,
2.50154000946738,2.53111678952409,2.53530707945431,2.53781800221899,2.53975412894107,
2.54184082857001,2.54514920602675,2.55598854329349,2.57373791311194,2.59396097058535),
 .UNSPECIFIED.);
#1804=B_SPLINE_CURVE_WITH_KNOTS('',3,(#171357,#171358,#171359,#171360,#171361,
#171362,#171363,#171364,#171365,#171366,#171367,#171368,#171369,#171370,
#171371,#171372,#171373,#171374,#171375,#171376,#171377,#171378,#171379,
#171380,#171381,#171382,#171383,#171384,#171385,#171386,#171387,#171388,
#171389,#171390,#171391,#171392,#171393,#171394,#171395,#171396,#171397,
#171398,#171399,#171400,#171401,#171402,#171403,#171404,#171405,#171406,
#171407,#171408,#171409,#171410,#171411,#171412,#171413,#171414,#171415,
#171416,#171417,#171418,#171419,#171420,#171421,#171422,#171423,#171424,
#171425,#171426,#171427,#171428,#171429,#171430,#171431,#171432,#171433,
#171434,#171435,#171436,#171437,#171438,#171439,#171440,#171441,#171442,
#171443,#171444,#171445,#171446,#171447,#171448,#171449,#171450,#171451,
#171452,#171453,#171454,#171455,#171456,#171457,#171458,#171459,#171460,
#171461,#171462,#171463,#171464,#171465,#171466,#171467,#171468,#171469,
#171470,#171471,#171472,#171473,#171474,#171475,#171476,#171477,#171478,
#171479,#171480,#171481,#171482,#171483,#171484,#171485,#171486,#171487,
#171488,#171489,#171490,#171491,#171492,#171493,#171494,#171495,#171496,
#171497,#171498,#171499,#171500,#171501,#171502,#171503,#171504,#171505,
#171506,#171507,#171508,#171509,#171510,#171511,#171512,#171513,#171514,
#171515,#171516,#171517,#171518,#171519,#171520,#171521,#171522,#171523,
#171524,#171525,#171526,#171527,#171528,#171529,#171530,#171531,#171532,
#171533,#171534,#171535,#171536,#171537,#171538,#171539,#171540,#171541,
#171542,#171543,#171544,#171545,#171546,#171547,#171548,#171549,#171550,
#171551,#171552,#171553,#171554,#171555,#171556,#171557,#171558,#171559,
#171560,#171561,#171562,#171563,#171564,#171565,#171566),.UNSPECIFIED.,
 .F.,.F.,(4,2,2,2,2,2,2,2,2,2,2,2,2,2,2,2,2,2,2,2,2,2,2,2,2,2,2,2,2,2,2,
2,2,2,2,2,2,2,2,2,2,2,2,2,2,2,2,2,2,2,2,2,2,2,2,2,2,2,2,2,2,2,2,2,2,2,2,
2,2,2,2,2,2,2,2,2,2,2,2,2,2,2,2,2,2,2,2,2,2,2,2,2,2,2,2,2,2,2,2,2,2,2,2,
2,4),(1.40817976059961,1.40954560798892,1.41147833503154,1.41357286057273,
1.41691845351314,1.42810815196938,1.44666701284211,1.49069806272605,1.49656815679459,
1.51244823560637,1.51506158353223,1.5164074462051,1.51747861916724,1.5187364018262,
1.52101503256817,1.53242866566733,1.55875511038331,1.61123424300218,1.61816336737727,
1.62103578224914,1.62282984569815,1.62479053755441,1.62749311448799,1.63388992588092,
1.68180166895086,1.72137451008661,1.72610764741294,1.7278508699183,1.72887685767718,
1.72996902105914,1.73147802721958,1.73505265857317,1.77422260144584,1.82298260616433,
1.83011270279042,1.83301845707072,1.83481857454488,1.83677417528322,1.83944854634883,
1.84568071219699,1.87272400329981,1.91345111090567,1.93614316951335,1.93899650693946,
1.9403732371886,1.94144691268922,1.94268259347209,1.94486021861204,1.95465270611566,
2.00353527789093,2.03864078780423,2.04293546813942,2.04547652497697,2.0474171577801,
2.04949047037842,2.05273924695119,2.06305117296332,2.07961732234454,2.1125076926792,
2.12707698170315,2.13238313539665,2.14842370753174,2.15104509069604,2.15239271963392,
2.15346399209599,2.15472035118399,2.15699274279259,2.16829978004372,2.19420723197035,
2.24727840870293,2.25416229203494,2.25702705254161,2.25881956785921,2.26078116514355,
2.2634897498175,2.26992328067746,2.29863209204647,2.34984120859534,2.36088056279273,
2.36302621553676,2.36438225315829,2.36545415330734,2.36670427012878,2.36894790980019,
2.37976748576411,2.4038168235839,2.4596399162556,2.46627675903133,2.46881789208597,
2.47064428867979,2.47252037775033,2.47500476100931,2.47774314421726,2.48229547136513,
2.49162801998579,2.54226197104376,2.57203627007789,2.57495064032719,2.57633925275901,
2.57741407538504,2.57864198807004,2.58078448298667,2.59007765633515,2.60891632639188,
2.66742169222757),.UNSPECIFIED.);
#1805=B_SPLINE_CURVE_WITH_KNOTS('',3,(#171567,#171568,#171569,#171570),
 .UNSPECIFIED.,.F.,.F.,(4,4),(-16.7565928429673,-16.4074096477818),
 .UNSPECIFIED.);
#1806=B_SPLINE_CURVE_WITH_KNOTS('',3,(#171576,#171577,#171578,#171579,#171580,
#171581,#171582,#171583,#171584,#171585,#171586,#171587,#171588,#171589,
#171590,#171591),.UNSPECIFIED.,.F.,.F.,(4,2,2,2,2,2,2,4),(2.593432104111,
2.64858655332197,2.65674930219105,2.65982049707518,2.66165177161212,2.66349570067702,
2.66578750456173,2.66785180667336),.UNSPECIFIED.);
#1807=B_SPLINE_CURVE_WITH_KNOTS('',3,(#171592,#171593,#171594,#171595,#171596,
#171597,#171598,#171599,#171600,#171601,#171602,#171603,#171604,#171605,
#171606,#171607,#171608,#171609,#171610,#171611,#171612,#171613,#171614,
#171615,#171616,#171617,#171618,#171619,#171620,#171621,#171622,#171623,
#171624,#171625,#171626,#171627,#171628,#171629,#171630,#171631,#171632,
#171633,#171634,#171635,#171636,#171637,#171638,#171639,#171640,#171641,
#171642,#171643,#171644,#171645,#171646,#171647,#171648,#171649,#171650,
#171651,#171652,#171653,#171654,#171655,#171656,#171657,#171658,#171659,
#171660,#171661,#171662,#171663,#171664,#171665,#171666,#171667,#171668,
#171669,#171670,#171671,#171672,#171673,#171674,#171675,#171676,#171677,
#171678,#171679,#171680,#171681,#171682,#171683,#171684,#171685,#171686,
#171687,#171688,#171689,#171690,#171691,#171692,#171693,#171694,#171695,
#171696,#171697,#171698,#171699,#171700,#171701,#171702,#171703,#171704,
#171705,#171706,#171707,#171708,#171709,#171710,#171711,#171712,#171713,
#171714,#171715,#171716,#171717,#171718,#171719,#171720,#171721,#171722,
#171723,#171724,#171725,#171726,#171727,#171728,#171729,#171730,#171731,
#171732,#171733,#171734,#171735,#171736,#171737,#171738,#171739,#171740,
#171741,#171742,#171743,#171744,#171745,#171746,#171747,#171748,#171749,
#171750,#171751,#171752,#171753,#171754,#171755,#171756,#171757,#171758,
#171759,#171760,#171761,#171762,#171763,#171764,#171765,#171766,#171767,
#171768,#171769,#171770,#171771,#171772,#171773,#171774,#171775,#171776,
#171777,#171778,#171779,#171780,#171781,#171782,#171783,#171784,#171785,
#171786,#171787,#171788,#171789,#171790,#171791,#171792,#171793,#171794,
#171795,#171796,#171797,#171798,#171799,#171800,#171801,#171802,#171803,
#171804,#171805,#171806,#171807,#171808,#171809,#171810,#171811,#171812,
#171813,#171814,#171815,#171816,#171817,#171818,#171819,#171820,#171821,
#171822,#171823,#171824,#171825,#171826,#171827,#171828,#171829,#171830,
#171831,#171832,#171833,#171834,#171835,#171836,#171837,#171838,#171839,
#171840,#171841,#171842,#171843,#171844,#171845),.UNSPECIFIED.,.F.,.F.,
(4,2,2,2,2,2,2,2,2,2,2,2,2,2,2,2,2,2,2,2,2,2,2,2,2,2,2,2,2,2,2,2,2,2,2,
2,2,2,2,2,2,2,2,2,2,2,2,2,2,2,2,2,2,2,2,2,2,2,2,2,2,2,2,2,2,2,2,2,2,2,2,
2,2,2,2,2,2,2,2,2,2,2,2,2,2,2,2,2,2,2,2,2,2,2,2,2,2,2,2,2,2,2,2,2,2,2,2,
2,2,2,2,2,2,2,2,2,2,2,2,2,2,2,2,2,2,2,4),(0.000823823589073982,0.00401009754324733,
0.0104659483184938,0.0609229667697557,0.0860113303179115,0.0971060554871067,
0.0993660887595639,0.100619741586636,0.101691241033782,0.10304238027135,
0.105680097639832,0.122145136882367,0.172110404056795,0.190191463422201,
0.201175885338313,0.203636754898609,0.205921840859828,0.205936427926701,
0.205951609293238,0.205967424553085,0.205983916850553,0.206001133630138,
0.206019127167111,0.206037954961812,0.206057680693129,0.206078375018293,
0.206100116615346,0.206122993333903,0.206147103683314,0.206172558526066,
0.206199483218856,0.206228020157709,0.206258331859729,0.206290604770655,
0.206325054226357,0.206361930827868,0.206401527780941,0.2064441892766,0.208321645320361,
0.210755871651084,0.215435397659435,0.250651908671031,0.299904881970501,
0.309294805197645,0.311444316535687,0.312673795009294,0.313748396883222,
0.315134616790653,0.31803656645619,0.350185389684556,0.382953121290837,
0.401774809307777,0.409258081551224,0.414880033872189,0.417445509367957,
0.419383103178602,0.421211590465703,0.423760175375085,0.430443801089756,
0.485860352738926,0.510210499873265,0.521110638551203,0.523359333814898,
0.524610629906711,0.52568253000632,0.527037267122833,0.529779493374406,
0.548228425699099,0.555160156134684,0.565632680004139,0.598466987138945,
0.614996067048697,0.62529265649893,0.628539969214722,0.63061316478851,0.63255426309132,
0.635096760958085,0.639395774357405,0.67478009936686,0.723968707593928,
0.733286290179115,0.735430903098509,0.73665945386373,0.737734465576581,
0.739122824163678,0.742034920542572,0.773631431240273,0.777736026984134,
0.810539671413484,0.833195206346511,0.83886263834764,0.841436793687725,
0.843376034235288,0.845202469710275,0.847742407903289,0.854368680439053,
0.910385235380532,0.934352020626436,0.945149898831714,0.947392735437358,
0.94864291006491,0.949715168119158,0.951072049505975,0.953219769852569,
0.96428591771816,1.0154324883676,1.04416133862173,1.05059874678806,1.05330852949945,
1.05527083909119,1.05706390229297,1.05992930251803,1.06681347281615,1.11996736034945,
1.14586858267119,1.15717501638262,1.15944796383811,1.16070470647357,1.16177636892278,
1.16312455750329,1.16574720186828,1.18179728296908,1.18590882563297,1.20160280711238,
1.23449513449812,1.25728609280512,1.26014274045541),.UNSPECIFIED.);
#1808=B_SPLINE_CURVE_WITH_KNOTS('',3,(#171847,#171848,#171849,#171850,#171851,
#171852,#171853,#171854,#171855,#171856),.UNSPECIFIED.,.F.,.F.,(4,1,1,1,
1,1,1,4),(-22.6905949549614,-21.9744018991612,-20.9755654491994,-19.9767289992375,
-18.9778925492756,-17.9790560993137,-16.9802196493519,-16.7565928429673),
 .UNSPECIFIED.);
#1809=B_SPLINE_CURVE_WITH_KNOTS('',3,(#171857,#171858,#171859,#171860,#171861,
#171862,#171863,#171864,#171865,#171866,#171867,#171868,#171869,#171870,
#171871,#171872,#171873,#171874),.UNSPECIFIED.,.F.,.F.,(4,2,2,2,2,2,2,2,
4),(0.000629331914479173,0.0468846876811639,0.0566532975426214,0.0588292040485486,
0.060064451053258,0.0611381007239059,0.062515249563224,0.0653710260823552,
0.0747567910363916),.UNSPECIFIED.);
#1810=B_SPLINE_CURVE_WITH_KNOTS('',3,(#171879,#171880,#171881,#171882,#171883,
#171884,#171885,#171886,#171887,#171888,#171889,#171890,#171891,#171892,
#171893,#171894,#171895,#171896,#171897,#171898,#171899,#171900,#171901,
#171902,#171903,#171904,#171905,#171906,#171907,#171908,#171909,#171910,
#171911,#171912,#171913,#171914,#171915,#171916,#171917,#171918,#171919,
#171920,#171921,#171922,#171923,#171924,#171925,#171926,#171927,#171928,
#171929,#171930,#171931,#171932,#171933,#171934,#171935,#171936,#171937,
#171938,#171939,#171940,#171941,#171942,#171943,#171944,#171945,#171946,
#171947,#171948,#171949,#171950,#171951,#171952,#171953,#171954,#171955,
#171956,#171957,#171958,#171959,#171960,#171961,#171962,#171963,#171964,
#171965,#171966,#171967,#171968,#171969,#171970,#171971,#171972,#171973,
#171974,#171975,#171976,#171977,#171978,#171979,#171980,#171981,#171982,
#171983,#171984,#171985,#171986,#171987,#171988,#171989,#171990,#171991,
#171992,#171993,#171994,#171995,#171996,#171997,#171998,#171999,#172000,
#172001,#172002,#172003,#172004,#172005,#172006,#172007,#172008,#172009,
#172010,#172011,#172012,#172013,#172014,#172015,#172016,#172017,#172018,
#172019,#172020,#172021,#172022,#172023,#172024,#172025,#172026,#172027,
#172028,#172029,#172030,#172031,#172032,#172033,#172034,#172035,#172036,
#172037,#172038,#172039,#172040,#172041,#172042,#172043,#172044,#172045,
#172046,#172047,#172048,#172049,#172050,#172051,#172052,#172053,#172054,
#172055,#172056,#172057,#172058,#172059,#172060,#172061,#172062,#172063,
#172064,#172065,#172066,#172067,#172068,#172069,#172070,#172071,#172072,
#172073,#172074,#172075,#172076,#172077,#172078,#172079,#172080,#172081,
#172082,#172083,#172084,#172085,#172086,#172087,#172088,#172089,#172090,
#172091,#172092,#172093,#172094,#172095,#172096,#172097,#172098,#172099,
#172100,#172101,#172102,#172103,#172104,#172105,#172106,#172107,#172108,
#172109,#172110,#172111,#172112,#172113,#172114),.UNSPECIFIED.,.F.,.F.,
(4,2,2,2,2,2,2,2,2,2,2,2,2,2,2,2,2,2,2,2,2,2,2,2,2,2,2,2,2,2,2,2,2,2,2,
2,2,2,2,2,2,2,2,2,2,2,2,2,2,2,2,2,2,2,2,2,2,2,2,2,2,2,2,2,2,2,2,2,2,2,2,
2,2,2,2,2,2,2,2,2,2,2,2,2,2,2,2,2,2,2,2,2,2,2,2,2,2,2,2,2,2,2,2,2,2,2,2,
2,2,2,2,2,2,2,2,2,2,4),(1.25989869578533,1.27803777571643,1.28162356492777,
1.28313446666498,1.28422693449528,1.28525230518831,1.28699267692713,1.29170757564036,
1.33211640603649,1.33400578949135,1.37783005827692,1.38505187095889,1.38797305507987,
1.38977603825891,1.39172949126977,1.39439149081119,1.40055211078964,1.42701754731372,
1.46593296247835,1.47407593030229,1.49134853466584,1.49401699056791,1.49537478041499,
1.49644684866122,1.49769576620184,1.49993375778852,1.51065957418799,1.53436265518954,
1.56173432592115,1.59366388420552,1.59790331481537,1.6004284182099,1.60236658671307,
1.60444676100264,1.60772628288389,1.61830771511249,1.63547407489022,1.68121297299587,
1.68797737603305,1.70342262003362,1.7057904745399,1.70719802739904,1.7082781674308,
1.70948161782518,1.71151344742636,1.71940427865583,1.73412119512362,1.76315957553927,
1.80554479278682,1.80983774025507,1.81237841472571,1.81431912623184,1.81639288268724,
1.81964310673741,1.82996598145874,1.84655579928852,1.87946737489397,1.89550907695404,
1.89932180907876,1.91533533736798,1.91795524474975,1.91930262868772,1.9203739678258,
1.9216307037395,1.92390457432152,1.93523530636968,1.96123440779445,2.01418044130187,
2.02107490612349,2.02394152494074,2.02573446421028,2.02769593144562,2.03040324713488,
2.03682860164504,2.06546697008432,2.11676194568742,2.127805999408,2.12995204042049,
2.13130824240475,2.13238022285594,2.13363037861163,2.13587393020343,2.14669005256395,
2.17072535207003,2.22657436422238,2.23321130725402,2.23575257505088,2.23757909894064,
2.23951763436412,2.24208948632968,2.24774625846598,2.27032990718819,2.30311153642334,
2.33903525050865,2.34189309223774,2.34327070004228,2.34434445197047,2.34557953664187,
2.34775447412086,2.35750779793843,2.40642295223264,2.44153144884381,2.4462092247807,
2.44864312953156,2.45051307210154,2.4525986609391,2.45478120837742,2.45799632070294,
2.4931273459558,2.54892180846205,2.55320147152664,2.55487402507419,2.55588626101695,
2.55698847717449,2.55855264167954,2.56246030563949,2.58162420589184,2.593432104111),
 .UNSPECIFIED.);
#1811=B_SPLINE_CURVE_WITH_KNOTS('',3,(#172115,#172116,#172117,#172118,#172119,
#172120,#172121,#172122,#172123,#172124,#172125,#172126,#172127,#172128,
#172129,#172130,#172131,#172132,#172133,#172134,#172135,#172136,#172137,
#172138,#172139,#172140,#172141,#172142,#172143,#172144,#172145,#172146,
#172147,#172148,#172149,#172150,#172151,#172152,#172153,#172154,#172155,
#172156,#172157,#172158,#172159,#172160,#172161,#172162,#172163,#172164,
#172165,#172166,#172167,#172168,#172169,#172170,#172171,#172172,#172173,
#172174,#172175,#172176,#172177,#172178,#172179,#172180,#172181,#172182,
#172183,#172184,#172185,#172186,#172187,#172188,#172189,#172190,#172191,
#172192,#172193,#172194,#172195,#172196,#172197,#172198,#172199,#172200,
#172201,#172202,#172203,#172204,#172205,#172206,#172207,#172208,#172209,
#172210,#172211,#172212,#172213,#172214,#172215,#172216,#172217,#172218,
#172219,#172220,#172221,#172222,#172223,#172224,#172225,#172226,#172227,
#172228,#172229,#172230,#172231,#172232,#172233,#172234,#172235,#172236,
#172237,#172238,#172239,#172240,#172241,#172242,#172243,#172244,#172245,
#172246,#172247,#172248,#172249,#172250,#172251,#172252,#172253,#172254,
#172255,#172256,#172257,#172258,#172259,#172260,#172261,#172262,#172263,
#172264,#172265,#172266,#172267,#172268,#172269,#172270,#172271,#172272,
#172273,#172274,#172275,#172276,#172277,#172278,#172279,#172280,#172281,
#172282,#172283,#172284,#172285,#172286,#172287,#172288,#172289,#172290,
#172291,#172292,#172293,#172294,#172295,#172296,#172297,#172298,#172299,
#172300,#172301,#172302,#172303,#172304,#172305,#172306,#172307,#172308,
#172309,#172310,#172311,#172312,#172313,#172314,#172315,#172316,#172317,
#172318,#172319,#172320,#172321,#172322,#172323,#172324,#172325,#172326,
#172327,#172328,#172329,#172330,#172331,#172332,#172333,#172334,#172335,
#172336,#172337,#172338,#172339,#172340,#172341,#172342,#172343,#172344,
#172345,#172346),.UNSPECIFIED.,.F.,.F.,(4,2,2,2,2,2,2,2,2,2,2,2,2,2,2,2,
2,2,2,2,2,2,2,2,2,2,2,2,2,2,2,2,2,2,2,2,2,2,2,2,2,2,2,2,2,2,2,2,2,2,2,2,
2,2,2,2,2,2,2,2,2,2,2,2,2,2,2,2,2,2,2,2,2,2,2,2,2,2,2,2,2,2,2,2,2,2,2,2,
2,2,2,2,2,2,2,2,2,2,2,2,2,2,2,2,2,2,2,2,2,2,2,2,2,2,2,4),(0.0747567910363916,
0.101524456188114,0.118346548840528,0.145432256689375,0.159880953081397,
0.163459317400085,0.165647666653395,0.167561843337173,0.169931194533515,
0.173564887856589,0.190666959648489,0.198773286722755,0.245100186900313,
0.260632355566143,0.268815353103309,0.270871847159655,0.272080733752706,
0.273159431087181,0.274556848020972,0.276890151957204,0.291506356757988,
0.299696300380568,0.34502341145215,0.362077704187808,0.372610104253377,
0.375884008462693,0.377962883583548,0.379901417889835,0.382429253110941,
0.386678305314137,0.419101082480044,0.458224706501592,0.472935778016126,
0.480823614708884,0.482855127579296,0.484058466147926,0.485138565467233,
0.48654612900863,0.488914132671086,0.504367042265317,0.508620048289381,
0.55660453872408,0.573910610266322,0.5845550577961,0.587841519528848,0.589923159197865,
0.591860656859772,0.594381984499563,0.59860868992616,0.629910818680944,
0.669588251031157,0.684726668285683,0.692769187121374,0.694813921609099,
0.696020203173269,0.697099552472877,0.698501702836229,0.700851153343846,
0.715850274499841,0.723372725573538,0.766610548811049,0.785190513985374,
0.796390695477342,0.799737676515783,0.801832694909756,0.803765623544705,
0.806257092661958,0.810381720935304,0.837505843098225,0.879435091935224,
0.896079190237384,0.904649081155813,0.906736988979772,0.907952878982071,
0.909030060660038,0.910415486231704,0.912707886900142,0.926461256037331,
0.92845511125291,0.929506506256935,0.973860518976542,1.0032293632098,1.00974182670138,
1.0124638652835,1.01442809703748,1.01621815767796,1.01906846476732,1.02586344113182,
1.0800715532697,1.10523451812109,1.11634943610266,1.11861090576434,1.11986498931481,
1.12093663326277,1.122287669134,1.12492433827512,1.14135478892318,1.19194117065031,
1.20965194988409,1.22047513781774,1.22378150584,1.22586761666604,1.22780366471858,
1.23031514840125,1.23450785801299,1.2642510280766,1.30519338753996,1.32767219399301,
1.33033551699752,1.33167430526232,1.33264224568188,1.33386581355116,1.33598825623172,
1.34500663884769,1.36299113618112,1.40819788515412),.UNSPECIFIED.);
#1812=B_SPLINE_CURVE_WITH_KNOTS('',3,(#172352,#172353,#172354,#172355,#172356,
#172357),.UNSPECIFIED.,.F.,.F.,(4,2,4),(2.59390093981336,2.60707187553918,
2.66837754069951),.UNSPECIFIED.);
#1813=B_SPLINE_CURVE_WITH_KNOTS('',3,(#172358,#172359,#172360,#172361,#172362,
#172363,#172364,#172365,#172366,#172367,#172368,#172369,#172370,#172371,
#172372,#172373,#172374,#172375,#172376,#172377,#172378,#172379,#172380,
#172381,#172382,#172383,#172384,#172385,#172386,#172387,#172388,#172389,
#172390,#172391,#172392,#172393,#172394,#172395,#172396,#172397,#172398,
#172399,#172400,#172401,#172402,#172403,#172404,#172405,#172406,#172407,
#172408,#172409,#172410,#172411,#172412,#172413,#172414,#172415,#172416,
#172417,#172418,#172419,#172420,#172421,#172422,#172423,#172424,#172425,
#172426,#172427,#172428,#172429,#172430,#172431,#172432,#172433,#172434,
#172435,#172436,#172437,#172438,#172439,#172440,#172441,#172442,#172443,
#172444,#172445,#172446,#172447,#172448,#172449,#172450,#172451,#172452,
#172453,#172454,#172455,#172456,#172457,#172458,#172459,#172460,#172461,
#172462,#172463,#172464,#172465,#172466,#172467,#172468,#172469,#172470,
#172471,#172472,#172473,#172474,#172475,#172476,#172477,#172478,#172479,
#172480,#172481,#172482,#172483,#172484,#172485,#172486,#172487,#172488,
#172489,#172490,#172491,#172492,#172493,#172494,#172495,#172496,#172497,
#172498,#172499,#172500,#172501,#172502,#172503,#172504,#172505,#172506,
#172507,#172508,#172509,#172510,#172511,#172512,#172513,#172514,#172515,
#172516,#172517,#172518,#172519,#172520,#172521,#172522,#172523,#172524,
#172525,#172526,#172527,#172528,#172529,#172530,#172531,#172532,#172533,
#172534,#172535,#172536,#172537,#172538,#172539,#172540,#172541,#172542,
#172543,#172544,#172545,#172546,#172547,#172548,#172549,#172550,#172551,
#172552,#172553,#172554,#172555,#172556,#172557,#172558,#172559,#172560,
#172561,#172562,#172563,#172564,#172565,#172566,#172567,#172568,#172569,
#172570,#172571,#172572,#172573,#172574,#172575,#172576,#172577,#172578,
#172579),.UNSPECIFIED.,.F.,.F.,(4,2,2,2,2,2,2,2,2,2,2,2,2,2,2,2,2,2,2,2,
2,2,2,2,2,2,2,2,2,2,2,2,2,2,2,2,2,2,2,2,2,2,2,2,2,2,2,2,2,2,2,2,2,2,2,2,
2,2,2,2,2,2,2,2,2,2,2,2,2,2,2,2,2,2,2,2,2,2,2,2,2,2,2,2,2,2,2,2,2,2,2,2,
2,2,2,2,2,2,2,2,2,2,2,2,2,2,2,2,2,2,4),(0.000810723700984357,0.00554261320572169,
0.00881069613611283,0.0102445762039883,0.0113189850637518,0.0123418017107931,
0.0133650037427745,0.0148060202972169,0.0186526222153408,0.0263910138025746,
0.0845154634150867,0.101772990584215,0.112395144693521,0.115678587832717,
0.117759219523011,0.119696406054065,0.122218222684451,0.126447724277269,
0.173069879744072,0.206916380206583,0.215664608440691,0.219322954632772,
0.221287249650054,0.222573677503932,0.223776849680925,0.22482590592252,
0.226194489868468,0.229007450046979,0.249970475940634,0.296516239281409,
0.320113757092421,0.325905911678698,0.328502109144104,0.33044413263795,
0.332263139443331,0.334776779899351,0.341243839866894,0.398654564430561,
0.421697202537265,0.43223953036286,0.4344659005549,0.435712141173873,0.436784282095004,
0.438145210124105,0.440307245485743,0.451618775422881,0.50268263979348,
0.531210900458154,0.537623037990028,0.540327828391182,0.542288575578362,
0.544081624667631,0.546950080227899,0.55385754424516,0.606640332115945,
0.632772141474778,0.644135100401236,0.646410562123642,0.6476675096593,0.648738627836554,
0.650085217047887,0.652200234739836,0.662760126223501,0.667525711208819,
0.675217676847446,0.688623006160559,0.721474362986219,0.74421396470811,
0.74989188453549,0.752467461194726,0.754406417472323,0.756231591622129,
0.758768184481559,0.765376370826019,0.821528588747223,0.845386821096472,
0.856153865520107,0.858394305382391,0.859643708330882,0.860715653031557,
0.862072585294457,0.864737252988573,0.88191157182582,0.92740438682891,0.955260646894826,
0.961592343664603,0.964283692718814,0.966242221573491,0.968038452126711,
0.970923412728924,0.977929436993805,1.02926394257437,1.05643268653373,1.06805495714825,
1.07034525125476,1.07160551861432,1.07267652835782,1.07401925675635,1.07661772789688,
1.09212829312262,1.09870253532691,1.14007976721838,1.16734411190291,1.17360381401307,
1.17628290258083,1.17823931534818,1.18003834465021,1.18293826439588,1.19003363050845,
1.23966140302115,1.25989869578533),.UNSPECIFIED.);
#1814=B_SPLINE_CURVE_WITH_KNOTS('',3,(#172581,#172582,#172583,#172584,#172585,
#172586,#172587,#172588,#172589,#172590,#172591,#172592,#172593,#172594,
#172595,#172596,#172597,#172598,#172599,#172600,#172601,#172602,#172603,
#172604,#172605,#172606,#172607,#172608,#172609,#172610,#172611,#172612,
#172613,#172614,#172615,#172616,#172617,#172618,#172619,#172620,#172621,
#172622,#172623,#172624,#172625,#172626,#172627,#172628,#172629,#172630,
#172631,#172632,#172633,#172634,#172635,#172636,#172637,#172638,#172639,
#172640,#172641,#172642,#172643,#172644,#172645,#172646,#172647,#172648,
#172649,#172650,#172651,#172652,#172653,#172654,#172655,#172656,#172657,
#172658,#172659,#172660,#172661,#172662,#172663,#172664,#172665,#172666,
#172667,#172668,#172669,#172670,#172671,#172672,#172673,#172674,#172675,
#172676,#172677,#172678,#172679,#172680,#172681,#172682,#172683,#172684,
#172685,#172686,#172687,#172688,#172689,#172690,#172691,#172692,#172693,
#172694,#172695,#172696,#172697,#172698,#172699,#172700,#172701,#172702,
#172703,#172704,#172705,#172706,#172707,#172708,#172709,#172710,#172711,
#172712,#172713,#172714,#172715,#172716,#172717,#172718,#172719,#172720,
#172721,#172722,#172723,#172724,#172725,#172726,#172727,#172728,#172729,
#172730,#172731,#172732,#172733,#172734,#172735,#172736,#172737,#172738,
#172739,#172740,#172741,#172742,#172743,#172744,#172745,#172746,#172747,
#172748,#172749,#172750,#172751,#172752,#172753,#172754,#172755,#172756,
#172757,#172758,#172759,#172760,#172761,#172762,#172763,#172764,#172765,
#172766,#172767,#172768,#172769,#172770,#172771,#172772,#172773,#172774,
#172775,#172776,#172777,#172778,#172779,#172780,#172781,#172782,#172783,
#172784,#172785,#172786,#172787,#172788,#172789,#172790,#172791,#172792,
#172793,#172794,#172795,#172796,#172797,#172798,#172799,#172800,#172801,
#172802,#172803,#172804,#172805,#172806,#172807,#172808),.UNSPECIFIED.,
 .F.,.F.,(4,2,2,2,2,2,2,2,2,2,2,2,2,2,2,2,2,2,2,2,2,2,2,2,2,2,2,2,2,2,2,
2,2,2,2,2,2,2,2,2,2,2,2,2,2,2,2,2,2,2,2,2,2,2,2,2,2,2,2,2,2,2,2,2,2,2,2,
2,2,2,2,2,2,2,2,2,2,2,2,2,2,2,2,2,2,2,2,2,2,2,2,2,2,2,2,2,2,2,2,2,2,2,2,
2,2,2,2,2,2,2,2,2,2,4),(1.40819788515412,1.41320480955033,1.43100805154192,
1.43468737730319,1.43707091781286,1.43898633702858,1.44116501332167,1.44488970303174,
1.46029553252312,1.51162818140741,1.5393065028968,1.5422133536684,1.5436006137059,
1.54467541768557,1.54590445995735,1.54805162669176,1.55740693895738,1.60667065956928,
1.64189277627461,1.64618928346868,1.64873098295828,1.65067185451119,1.652745178032,
1.6559934624727,1.66629954363591,1.68285225744042,1.71573289764331,1.72917870687183,
1.73676473242227,1.75176082213401,1.75411020406588,1.75551233516349,1.75659168476984,
1.75779799561915,1.75984282695774,1.76788652127728,1.78302608529412,1.8227323590549,
1.85396287365098,1.85818793187896,1.86070881328773,1.86264627009395,1.86472816143071,
1.86801564589376,1.87866880699907,1.89599683009939,1.94421862210615,1.94852171496344,
1.95176755675804,1.96398266332999,1.96619652137505,1.96757330590134,1.96864703367207,
1.96988278797529,1.97206057371562,1.98185431033581,2.03073864750066,2.06584379556519,
2.07013863983217,2.07267980745666,2.07462053312108,2.07669395313408,2.07994291562159,
2.090255589143,2.1068231165886,2.13971533624545,2.15436242289754,2.15958048548214,
2.17562924673426,2.17825123591975,2.17959903316586,2.18067035545633,2.181926671319,
2.18419876504807,2.19549982453134,2.22138329857757,2.27449172343357,2.28137310471485,
2.28423749466763,2.28602997251859,2.28799168504442,2.29070071537147,2.29713666181787,
2.306024990725,2.35723578537287,2.38723379368933,2.39014813385419,2.39153676628313,
2.39261161996421,2.39383958551193,2.39598221501358,2.40527662675433,2.42411888605869,
2.47030817984565,2.47176799657821,2.49079024426924,2.49454973560932,2.49695784527914,
2.49887534941399,2.50067253519439,2.50376503716656,2.51330922614352,2.52830875451936,
2.55060007977405,2.59664756030106,2.60129276543145,2.60302251666345,2.60404578508964,
2.60513955821508,2.60665806800296,2.61028885532386,2.61539962203938,2.62956644507116,
2.66719749894963),.UNSPECIFIED.);
#1815=B_SPLINE_CURVE_WITH_KNOTS('',3,(#172809,#172810,#172811,#172812,#172813,
#172814,#172815,#172816,#172817,#172818,#172819,#172820,#172821,#172822,
#172823,#172824,#172825,#172826,#172827,#172828),.UNSPECIFIED.,.F.,.F.,
(4,2,2,2,2,2,2,2,2,4),(0.000704185054399313,0.0257176001801729,0.0359848483797077,
0.0390635712064609,0.0411898671505945,0.04327101724974,0.0452083777863691,
0.0477299809557773,0.0519581517589747,0.0751489472892387),.UNSPECIFIED.);
#1816=B_SPLINE_CURVE_WITH_KNOTS('',3,(#172833,#172834,#172835,#172836,#172837,
#172838,#172839,#172840,#172841,#172842,#172843,#172844,#172845,#172846,
#172847,#172848,#172849,#172850,#172851,#172852,#172853,#172854,#172855,
#172856,#172857,#172858,#172859,#172860,#172861,#172862,#172863,#172864,
#172865,#172866,#172867,#172868,#172869,#172870,#172871,#172872,#172873,
#172874,#172875,#172876,#172877,#172878,#172879,#172880,#172881,#172882,
#172883,#172884,#172885,#172886,#172887,#172888,#172889,#172890,#172891,
#172892,#172893,#172894,#172895,#172896,#172897,#172898,#172899,#172900,
#172901,#172902,#172903,#172904,#172905,#172906,#172907,#172908,#172909,
#172910,#172911,#172912,#172913,#172914,#172915,#172916,#172917,#172918,
#172919,#172920,#172921,#172922,#172923,#172924,#172925,#172926,#172927,
#172928,#172929,#172930,#172931,#172932,#172933,#172934,#172935,#172936,
#172937,#172938,#172939,#172940,#172941,#172942,#172943,#172944,#172945,
#172946,#172947,#172948,#172949,#172950,#172951,#172952,#172953,#172954,
#172955,#172956,#172957,#172958,#172959,#172960,#172961,#172962,#172963,
#172964,#172965,#172966,#172967,#172968,#172969,#172970,#172971,#172972,
#172973,#172974,#172975,#172976,#172977,#172978,#172979,#172980,#172981,
#172982,#172983,#172984,#172985,#172986,#172987,#172988,#172989,#172990,
#172991,#172992,#172993,#172994,#172995,#172996,#172997,#172998,#172999,
#173000,#173001,#173002,#173003,#173004,#173005,#173006,#173007,#173008,
#173009,#173010,#173011,#173012,#173013,#173014,#173015,#173016,#173017,
#173018,#173019,#173020,#173021,#173022,#173023,#173024,#173025,#173026,
#173027,#173028,#173029,#173030,#173031,#173032,#173033,#173034,#173035,
#173036,#173037,#173038,#173039,#173040,#173041,#173042,#173043,#173044,
#173045,#173046,#173047,#173048,#173049,#173050,#173051,#173052,#173053,
#173054,#173055,#173056,#173057,#173058,#173059,#173060,#173061,#173062,
#173063,#173064,#173065,#173066,#173067,#173068,#173069,#173070,#173071,
#173072,#173073,#173074,#173075,#173076,#173077,#173078,#173079,#173080,
#173081,#173082,#173083,#173084,#173085,#173086,#173087,#173088,#173089,
#173090,#173091,#173092,#173093,#173094,#173095,#173096,#173097,#173098,
#173099,#173100,#173101,#173102,#173103,#173104),.UNSPECIFIED.,.F.,.F.,
(4,2,2,2,2,2,2,2,2,2,2,2,2,2,2,2,2,2,2,2,2,2,2,2,2,2,2,2,2,2,2,2,2,2,2,
2,2,2,2,2,2,2,2,2,2,2,2,2,2,2,2,2,2,2,2,2,2,2,2,2,2,2,2,2,2,2,2,2,2,2,2,
2,2,2,2,2,2,2,2,2,2,2,2,2,2,2,2,2,2,2,2,2,2,2,2,2,2,2,2,2,2,2,2,2,2,2,2,
2,2,2,2,2,2,2,2,2,2,2,2,2,2,2,2,2,2,2,2,2,2,2,2,2,2,2,2,4),(1.26009529204153,
1.26844197493161,1.29381908665805,1.29808977294706,1.30038729580617,1.30228035921571,
1.30452109389515,1.30842023916197,1.32432886191597,1.33455106590784,1.3738352565579,
1.4024193346263,1.40533187738955,1.40672042186942,1.40779556129193,1.40902424908107,
1.41116906596271,1.42048729387565,1.46966352868001,1.50503251890401,1.50933167680465,
1.51187442603891,1.51381580080436,1.51588937269098,1.51913744272381,1.52943776213862,
1.54597639320325,1.57352305450409,1.58966610161661,1.60074910637597,1.61498196810458,
1.61729842640309,1.61869106011059,1.6197693270595,1.62098139213644,1.62305141293665,
1.63139524163988,1.6473807097364,1.68969665771436,1.71730662606135,1.72144413217767,
1.72393965127285,1.72587350083235,1.72796729970624,1.73130752743709,1.74244013679484,
1.76086405966356,1.80763034731911,1.81232709764671,1.82696406662867,1.82929874004238,
1.83069673086658,1.8317757227877,1.83298478601298,1.83504122555829,1.84321961617839,
1.85873479280358,1.90015323793686,1.90975608772036,1.92990197006417,1.9337241801803,
1.93615182087995,1.93807174021844,1.94022284482432,1.94382155599842,1.95765691707316,
2.00858847432579,2.03848478022232,2.04140011095768,2.04278919146687,2.04386438098087,
2.04509271791304,2.04723596667405,2.05653262121604,2.07537870364252,2.11578208748357,
2.1280448874829,2.1426640883555,2.14645403678354,2.14866967292115,2.15058229072505,
2.15291750737014,2.15736701469366,2.18823827194742,2.2346751533935,2.25091584498385,
2.25354556935495,2.25489531762309,2.25596712881483,2.25722278915879,2.25949058324815,
2.27070702311502,2.29625407243746,2.34988213657719,2.35672626840969,2.35958516041191,
2.36137710810909,2.36334058690595,2.3660563714244,2.37252891301422,2.42683246281601,
2.46271444433038,2.46557632123003,2.46695503000674,2.4679977587146,2.46800240941345,
2.46800697901051,2.46801146932995,2.4680158820592,2.46802021881731,2.468024481455,
2.46802867152553,2.4680327904781,2.4680368398472,2.46804082120923,2.46804473593346,
2.46804858533323,2.46805217845779,2.46805575817054,2.46805932453551,2.46806287762952,
2.46928594144211,2.47059639747212,2.47261801169278,2.47642684073078,2.48568673577153,
2.52344240916099,2.5331599780408,2.56531506690709,2.56956000770442,2.57208710202107,
2.57402604819646,2.57610632274238,2.5793844513405,2.5899478892837,2.59390093981336),
 .UNSPECIFIED.);
#1817=B_SPLINE_CURVE_WITH_KNOTS('',3,(#173105,#173106,#173107,#173108,#173109,
#173110,#173111,#173112,#173113,#173114,#173115,#173116,#173117,#173118,
#173119,#173120,#173121,#173122,#173123,#173124,#173125,#173126,#173127,
#173128,#173129,#173130,#173131,#173132,#173133,#173134,#173135,#173136,
#173137,#173138,#173139,#173140,#173141,#173142,#173143,#173144,#173145,
#173146,#173147,#173148,#173149,#173150,#173151,#173152,#173153,#173154,
#173155,#173156,#173157,#173158,#173159,#173160,#173161,#173162,#173163,
#173164,#173165,#173166,#173167,#173168,#173169,#173170,#173171,#173172,
#173173,#173174,#173175,#173176,#173177,#173178,#173179,#173180,#173181,
#173182,#173183,#173184,#173185,#173186,#173187,#173188,#173189,#173190,
#173191,#173192,#173193,#173194,#173195,#173196,#173197,#173198,#173199,
#173200,#173201,#173202,#173203,#173204,#173205,#173206,#173207,#173208,
#173209,#173210,#173211,#173212,#173213,#173214,#173215,#173216,#173217,
#173218,#173219,#173220,#173221,#173222,#173223,#173224,#173225,#173226,
#173227,#173228,#173229,#173230,#173231,#173232,#173233,#173234,#173235,
#173236,#173237,#173238,#173239,#173240,#173241,#173242,#173243,#173244,
#173245,#173246,#173247,#173248,#173249,#173250,#173251,#173252,#173253,
#173254,#173255,#173256,#173257,#173258,#173259,#173260,#173261,#173262,
#173263,#173264,#173265,#173266,#173267,#173268,#173269,#173270,#173271,
#173272,#173273,#173274,#173275,#173276,#173277,#173278,#173279,#173280,
#173281,#173282,#173283,#173284,#173285,#173286,#173287,#173288,#173289,
#173290,#173291,#173292,#173293,#173294,#173295,#173296,#173297,#173298,
#173299,#173300,#173301,#173302,#173303,#173304,#173305,#173306,#173307,
#173308,#173309,#173310,#173311,#173312,#173313,#173314,#173315,#173316,
#173317,#173318,#173319,#173320,#173321,#173322,#173323,#173324,#173325,
#173326,#173327,#173328,#173329,#173330,#173331,#173332,#173333,#173334),
 .UNSPECIFIED.,.F.,.F.,(4,2,2,2,2,2,2,2,2,2,2,2,2,2,2,2,2,2,2,2,2,2,2,2,
2,2,2,2,2,2,2,2,2,2,2,2,2,2,2,2,2,2,2,2,2,2,2,2,2,2,2,2,2,2,2,2,2,2,2,2,
2,2,2,2,2,2,2,2,2,2,2,2,2,2,2,2,2,2,2,2,2,2,2,2,2,2,2,2,2,2,2,2,2,2,2,2,
2,2,2,2,2,2,2,2,2,2,2,2,2,2,2,2,2,2,4),(0.0751489472892387,0.0833506903298647,
0.108693179478461,0.136624479574853,0.145910581493636,0.148052443073946,
0.149280142392567,0.150354881899416,0.151743512998436,0.153997122734652,
0.16697267146495,0.188669927722425,0.21538790536825,0.23698283912962,0.245199084137935,
0.251208117972463,0.253835202657818,0.255791748353884,0.257590251491323,
0.260487889091777,0.267570463669636,0.317768473763119,0.35556512818206,
0.359164548317838,0.360677695364973,0.361770484303532,0.362795121015494,
0.364532042274383,0.369224770895711,0.410121627603691,0.456727760812597,
0.463120295750263,0.465821963995688,0.46778232474392,0.469576314887164,
0.472449100333618,0.479381604657555,0.53183102652881,0.558205007536708,
0.569629676589747,0.571908849257935,0.57316669435742,0.574237879798275,
0.575583666863853,0.578196353888663,0.594048508720194,0.598800004794369,
0.614070759120716,0.646946875496303,0.663528766522946,0.673848955191107,
0.677098762767563,0.679172362956032,0.681113005616564,0.683653702799897,
0.687946973484252,0.730347412354117,0.759404062666403,0.774125704647657,
0.782017411858803,0.784049267769345,0.785252687682802,0.786332774959836,
0.787740211173355,0.790107761588505,0.805548807216033,0.812259157611298,
0.826060037640182,0.858920747327703,0.875483046744663,0.885794498952606,
0.889043394098526,0.891116853804617,0.893057675231676,0.895599054028324,
0.89989447953962,0.935013678434636,0.983922775958131,0.993722716270286,
0.995901057091978,0.997136987612726,0.998210784689413,0.999587539076382,
1.00244049216916,1.02510696755175,1.03806638041779,1.07092231103286,1.0874764009265,
1.09778443824991,1.10103316035812,1.10310672663729,1.10504780027098,1.10758972929978,
1.11188657793559,1.14708330643099,1.19623165405848,1.20575819674281,1.20791776643048,
1.20914964803851,1.21022418219166,1.21160746587854,1.21384242657101,1.22644656507153,
1.23298155019536,1.23811527952155,1.27817831512221,1.30768219107849,1.31209262371577,
1.31441956312134,1.31614666045631,1.31830310095657,1.32192594696099,1.33437674435756,
1.38533771546958,1.40863959751122),.UNSPECIFIED.);
#1818=B_SPLINE_CURVE_WITH_KNOTS('',3,(#173340,#173341,#173342,#173343,#173344,
#173345,#173346,#173347,#173348,#173349),.UNSPECIFIED.,.F.,.F.,(4,2,2,2,
4),(2.59331024535127,2.59403892110998,2.60403517669797,2.65275213854603,
2.66748114715309),.UNSPECIFIED.);
#1819=B_SPLINE_CURVE_WITH_KNOTS('',3,(#173350,#173351,#173352,#173353,#173354,
#173355,#173356,#173357,#173358,#173359,#173360,#173361,#173362,#173363,
#173364,#173365,#173366,#173367,#173368,#173369,#173370,#173371,#173372,
#173373,#173374,#173375,#173376,#173377,#173378,#173379,#173380,#173381,
#173382,#173383,#173384,#173385,#173386,#173387,#173388,#173389,#173390,
#173391,#173392,#173393,#173394,#173395,#173396,#173397,#173398,#173399,
#173400,#173401,#173402,#173403,#173404,#173405,#173406,#173407,#173408,
#173409,#173410,#173411,#173412,#173413,#173414,#173415,#173416,#173417,
#173418,#173419,#173420,#173421,#173422,#173423,#173424,#173425,#173426,
#173427,#173428,#173429,#173430,#173431,#173432,#173433,#173434,#173435,
#173436,#173437,#173438,#173439,#173440,#173441,#173442,#173443,#173444,
#173445,#173446,#173447,#173448,#173449,#173450,#173451,#173452,#173453,
#173454,#173455,#173456,#173457,#173458,#173459,#173460,#173461,#173462,
#173463,#173464,#173465,#173466,#173467,#173468,#173469,#173470,#173471,
#173472,#173473,#173474,#173475,#173476,#173477,#173478,#173479,#173480,
#173481,#173482,#173483,#173484,#173485,#173486,#173487,#173488,#173489,
#173490,#173491,#173492,#173493,#173494,#173495,#173496,#173497,#173498,
#173499,#173500,#173501,#173502,#173503,#173504,#173505,#173506,#173507,
#173508,#173509,#173510,#173511,#173512,#173513,#173514,#173515,#173516,
#173517,#173518,#173519,#173520,#173521,#173522,#173523,#173524,#173525,
#173526,#173527,#173528,#173529,#173530,#173531,#173532,#173533,#173534,
#173535,#173536,#173537,#173538,#173539,#173540,#173541,#173542,#173543,
#173544,#173545,#173546,#173547,#173548,#173549,#173550,#173551,#173552,
#173553,#173554,#173555,#173556,#173557,#173558,#173559,#173560,#173561,
#173562,#173563,#173564,#173565,#173566,#173567,#173568,#173569,#173570,
#173571,#173572,#173573,#173574,#173575,#173576,#173577,#173578,#173579),
 .UNSPECIFIED.,.F.,.F.,(4,2,2,2,2,2,2,2,2,2,2,2,2,2,2,2,2,2,2,2,2,2,2,2,
2,2,2,2,2,2,2,2,2,2,2,2,2,2,2,2,2,2,2,2,2,2,2,2,2,2,2,2,2,2,2,2,2,2,2,2,
2,2,2,2,2,2,2,2,2,2,2,2,2,2,2,2,2,2,2,2,2,2,2,2,2,2,2,2,2,2,2,2,2,2,2,2,
2,2,2,2,2,2,2,2,2,2,2,2,2,2,2,2,2,2,4),(0.000768636914663262,0.0205817132677007,
0.0241264022558527,0.026446080246186,0.028288539982056,0.0301791844248606,
0.0323538709578556,0.0360614126099366,0.049342268561374,0.061439469886042,
0.106920494045923,0.123352098338178,0.131848845865215,0.13393077347796,
0.135145246475461,0.136222568716977,0.137609978393136,0.139909404628916,
0.153812066318087,0.165109782804785,0.176052200725826,0.208884599686808,
0.225415111063631,0.232254426277596,0.237451466882633,0.239925174807285,
0.241763389965213,0.243586282406605,0.246113909055398,0.252665291008623,
0.30933679523107,0.332864760921927,0.343541974817081,0.345777015734982,
0.347025293118148,0.348097439213071,0.349456126762224,0.351610368308616,
0.362788846072325,0.413971378521812,0.44254087089606,0.448958497584014,
0.45166452002466,0.453625766366755,0.455419000618713,0.458287161407423,
0.465190855672874,0.518047399066889,0.544139800981525,0.555493658326147,
0.557768904828446,0.559025948816909,0.560097279759711,0.561444302573145,
0.564062478863939,0.580044465753803,0.585011842731264,0.629859531159875,
0.648373658759317,0.659545647407061,0.662889680195208,0.664984078341141,
0.666917267473081,0.669410236886387,0.673539868929175,0.70085739816818,
0.74313635257933,0.759386683810092,0.767821327391028,0.769898481825624,
0.771112004744916,0.772189727806955,0.773579262729555,0.775885560930745,
0.789924643106426,0.791267448697257,0.798277731012625,0.811953601280656,
0.844814457685017,0.861375925978386,0.87168712574952,0.874936082465282,
0.877009615376341,0.878950529147309,0.881492063235158,0.885787828271423,
0.92091998429791,0.969866143718762,0.979625110904711,0.981800719637479,
0.983036082909888,0.984110016300242,0.985487767876626,0.988345616264717,
1.01120495290628,1.02397087336264,1.05682646448888,1.07337913078648,1.08368664822321,
1.08693540174869,1.08900903502374,1.09095020435551,1.09349230630476,1.09778955396186,
1.1330040871773,1.1822091972939,1.19167318002121,1.19382839647008,1.19505935262069,
1.19613408823427,1.19751895765512,1.19975907997433,1.21246035582909,1.23483790921113,
1.26009529204153),.UNSPECIFIED.);
#1820=B_SPLINE_CURVE_WITH_KNOTS('',3,(#173581,#173582,#173583,#173584,#173585,
#173586,#173587,#173588,#173589,#173590,#173591,#173592,#173593,#173594,
#173595,#173596,#173597,#173598,#173599,#173600,#173601,#173602,#173603,
#173604,#173605,#173606,#173607,#173608,#173609,#173610,#173611,#173612,
#173613,#173614,#173615,#173616,#173617,#173618,#173619,#173620,#173621,
#173622,#173623,#173624,#173625,#173626,#173627,#173628,#173629,#173630,
#173631,#173632,#173633,#173634,#173635,#173636,#173637,#173638,#173639,
#173640,#173641,#173642,#173643,#173644,#173645,#173646,#173647,#173648,
#173649,#173650,#173651,#173652,#173653,#173654,#173655,#173656,#173657,
#173658,#173659,#173660,#173661,#173662,#173663,#173664,#173665,#173666,
#173667,#173668,#173669,#173670,#173671,#173672,#173673,#173674,#173675,
#173676,#173677,#173678,#173679,#173680,#173681,#173682,#173683,#173684,
#173685,#173686,#173687,#173688,#173689,#173690,#173691,#173692,#173693,
#173694,#173695,#173696,#173697,#173698,#173699,#173700,#173701,#173702,
#173703,#173704,#173705,#173706,#173707,#173708,#173709,#173710,#173711,
#173712,#173713,#173714,#173715,#173716,#173717,#173718,#173719,#173720,
#173721,#173722,#173723,#173724,#173725,#173726,#173727,#173728,#173729,
#173730,#173731,#173732,#173733,#173734,#173735,#173736,#173737,#173738,
#173739,#173740,#173741,#173742,#173743,#173744,#173745,#173746,#173747,
#173748,#173749,#173750,#173751,#173752,#173753,#173754,#173755,#173756,
#173757,#173758,#173759,#173760,#173761,#173762,#173763,#173764,#173765,
#173766,#173767,#173768,#173769,#173770,#173771,#173772,#173773,#173774,
#173775,#173776,#173777,#173778,#173779,#173780,#173781,#173782,#173783,
#173784,#173785,#173786,#173787,#173788,#173789,#173790,#173791,#173792,
#173793,#173794,#173795,#173796,#173797,#173798,#173799,#173800,#173801,
#173802),.UNSPECIFIED.,.F.,.F.,(4,2,2,2,2,2,2,2,2,2,2,2,2,2,2,2,2,2,2,2,
2,2,2,2,2,2,2,2,2,2,2,2,2,2,2,2,2,2,2,2,2,2,2,2,2,2,2,2,2,2,2,2,2,2,2,2,
2,2,2,2,2,2,2,2,2,2,2,2,2,2,2,2,2,2,2,2,2,2,2,2,2,2,2,2,2,2,2,2,2,2,2,2,
2,2,2,2,2,2,2,2,2,2,2,2,2,2,2,2,2,2,4),(1.40863959751122,1.41654759067579,
1.41946078381403,1.42084944450047,1.42192458464356,1.42315317340584,1.42529758347594,
1.43461042542615,1.48376959661748,1.5191601098776,1.52345947761638,1.52600227178987,
1.52794363529235,1.53001715098209,1.53326504082311,1.54356401310051,1.56009974390899,
1.59297017588028,1.60449587310241,1.61425425826926,1.61606576418613,1.62921191722976,
1.63147476742771,1.63286642133205,1.63394180950153,1.63516837213546,1.63730385572504,
1.64649544979417,1.66501336722716,1.70917978599597,1.73178633348039,1.73573586227892,
1.73820212937626,1.74012635122654,1.74225532216663,1.74575440825437,1.75847661449871,
1.78077943937613,1.82579017005966,1.82762712554879,1.84118669695806,1.84347004156279,
1.84485293422678,1.84592998128415,1.84714779953147,1.84924371411316,1.85791204470865,
1.87484183103985,1.91719759816998,1.94351200520008,1.94761628936432,1.95010205233999,
1.95203446662113,1.95413284985835,1.95749374744105,1.96882119406152,1.98770007500022,
2.01701249497808,2.05265810089185,2.05552162619937,2.05690053739703,2.05797463164986,
2.05920935040837,2.06138182983116,2.07109429955398,2.12005725862705,2.15519127292122,
2.15948716125025,2.16202885601732,2.16396993208504,2.16604367586266,2.16929304002328,
2.17960609773535,2.1961733948144,2.22906873476792,2.26467869901025,2.26754489693501,
2.26892430287168,2.26999841142197,2.27123272833024,2.27340350338935,2.28309202634423,
2.33207329946603,2.3672124659043,2.37150828505844,2.37404991356645,2.37599092444375,
2.3780645844294,2.38131378776061,2.39162608602794,2.40819192620058,2.47083284402741,
2.47219421687869,2.47836789584991,2.48030628444921,2.48148909542873,2.48252076879123,
2.48393385037511,2.48694890762154,2.49104708912107,2.50132546172915,2.52414790866332,
2.57586043076164,2.58284430851619,2.58572619525003,2.58752230324613,2.58948213431421,
2.59217787903489,2.59853205712364,2.62656945764179,2.66826062582537),
 .UNSPECIFIED.);
#1821=B_SPLINE_CURVE_WITH_KNOTS('',3,(#173803,#173804,#173805,#173806,#173807,
#173808,#173809,#173810,#173811,#173812,#173813,#173814,#173815),
 .UNSPECIFIED.,.F.,.F.,(4,3,3,3,4),(-48.174029021668,-48.070804166684,-47.9674104177172,
-47.94414959817,-47.8233361836797),.UNSPECIFIED.);
#1822=B_SPLINE_CURVE_WITH_KNOTS('',3,(#173820,#173821,#173822,#173823,#173824,
#173825,#173826,#173827,#173828,#173829,#173830,#173831,#173832,#173833,
#173834,#173835,#173836,#173837,#173838,#173839,#173840,#173841,#173842,
#173843,#173844,#173845,#173846,#173847,#173848,#173849,#173850,#173851,
#173852,#173853,#173854,#173855,#173856,#173857,#173858,#173859,#173860,
#173861,#173862,#173863,#173864,#173865,#173866,#173867,#173868,#173869,
#173870,#173871,#173872,#173873,#173874,#173875,#173876,#173877,#173878,
#173879,#173880,#173881,#173882,#173883,#173884,#173885,#173886,#173887,
#173888,#173889,#173890,#173891,#173892,#173893,#173894,#173895,#173896,
#173897,#173898,#173899,#173900,#173901,#173902,#173903,#173904,#173905,
#173906,#173907,#173908,#173909,#173910,#173911,#173912,#173913,#173914,
#173915,#173916,#173917,#173918,#173919,#173920,#173921,#173922,#173923,
#173924,#173925,#173926,#173927,#173928,#173929,#173930,#173931,#173932,
#173933,#173934,#173935,#173936,#173937,#173938,#173939,#173940,#173941,
#173942,#173943,#173944,#173945,#173946,#173947,#173948,#173949,#173950,
#173951,#173952,#173953,#173954,#173955,#173956,#173957,#173958,#173959,
#173960,#173961,#173962,#173963,#173964,#173965,#173966,#173967,#173968,
#173969,#173970,#173971,#173972,#173973,#173974,#173975,#173976,#173977,
#173978,#173979,#173980,#173981,#173982,#173983,#173984,#173985,#173986,
#173987,#173988,#173989,#173990,#173991,#173992,#173993,#173994,#173995,
#173996,#173997,#173998,#173999,#174000,#174001,#174002,#174003,#174004,
#174005,#174006,#174007,#174008,#174009,#174010,#174011,#174012,#174013,
#174014,#174015,#174016,#174017,#174018,#174019,#174020,#174021,#174022,
#174023,#174024,#174025,#174026,#174027,#174028,#174029,#174030,#174031,
#174032,#174033,#174034,#174035,#174036,#174037,#174038,#174039,#174040,
#174041,#174042,#174043,#174044,#174045,#174046,#174047,#174048,#174049,
#174050,#174051,#174052,#174053,#174054,#174055,#174056,#174057,#174058,
#174059,#174060,#174061,#174062,#174063,#174064,#174065,#174066,#174067,
#174068,#174069,#174070,#174071,#174072,#174073,#174074,#174075,#174076,
#174077,#174078,#174079,#174080,#174081,#174082,#174083,#174084,#174085,
#174086,#174087,#174088,#174089,#174090,#174091,#174092,#174093,#174094,
#174095,#174096,#174097),.UNSPECIFIED.,.F.,.F.,(4,2,2,2,2,2,2,2,2,2,2,2,
2,2,2,2,2,2,2,2,2,2,2,2,2,2,2,2,2,2,2,2,2,2,2,2,2,2,2,2,2,2,2,2,2,2,2,2,
2,2,2,2,2,2,2,2,2,2,2,2,2,2,2,2,2,2,2,2,2,2,2,2,2,2,2,2,2,2,2,2,2,2,2,2,
2,2,2,2,2,2,2,2,2,2,2,2,2,2,2,2,2,2,2,2,2,2,2,2,2,2,2,2,2,2,2,2,2,2,2,2,
2,2,2,2,2,2,2,2,2,2,2,2,2,2,2,2,2,2,4),(1.25968337114772,1.2815038271417,
1.30395449861653,1.31433172173624,1.31654812649059,1.31779241236542,1.31886513648359,
1.3202297307965,1.32240314089473,1.33389984160313,1.38263543117029,1.41583871239245,
1.42010256654869,1.42263485781704,1.42457427825447,1.42665163350888,1.42991794424423,
1.44038100612086,1.45728195988552,1.4951104704737,1.52518584386112,1.52810043536703,
1.52948921209973,1.53056418877032,1.53179230746531,1.53393523378377,1.54323138971984,
1.56207793156719,1.60247840619797,1.61474050023896,1.62934633499325,1.63313461249557,
1.63534960205452,1.63726186138475,1.63959689136195,1.64404681498353,1.6749595661705,
1.72180667657544,1.73760388660089,1.74021636783017,1.74156225191304,1.74263362124364,
1.74389181171071,1.74617192993923,1.75760855126144,1.78402412413786,1.8363876377799,
1.84332608739892,1.84620016798932,1.84799462809362,1.84995523677239,1.85265675350369,
1.85904659407297,1.88738476591629,1.93728374955004,1.94991435750901,1.95215064902386,
1.95353428505236,1.95460879454741,1.95584032166545,1.95799848444546,1.96750662676836,
2.0166416983383,2.05182797042851,2.05612433189675,2.05866609436234,2.06060709991379,
2.06268064986615,2.06592946293961,2.07623868658228,2.09279784143566,2.12568538566885,
2.13955063270457,2.14611512615142,2.16166395047815,2.16426432974732,2.16560755858078,
2.16667870974449,2.16793884888367,2.17022814395277,2.18182963807436,2.20890920763088,
2.26033579694686,2.26733477660799,2.27021876841521,2.27201496933338,2.27397392917665,
2.27666670546291,2.28300563263239,2.31092245379032,2.35691745824166,2.35824204545841,
2.37368848034884,2.37605644184807,2.37746405043135,2.37854422847606,2.37974771597112,
2.38177959680905,2.38967048629553,2.40438732566613,2.44551765277643,2.47594527327307,
2.48016410013322,2.48268325980229,2.4846205585698,2.48469624893075,2.48474205912219,
2.4847863396922,2.48482649075229,2.48486295713526,2.48489612660784,2.4849263384659,
2.48495389225001,2.48497905121499,2.48500204816063,2.48502308959494,2.48504235924239,
2.48506002098396,2.48507622139417,2.48509898188053,2.48512131832721,2.4851432424048,
2.48516476901952,2.48518591096378,2.48520668057027,2.4852270896672,2.48524714957789,
2.48750337741587,2.49161502728447,2.49674798922724,2.50777813094903,2.53230016490609,
2.54786764107018,2.58533209066512,2.58816295458493,2.58953532329599,2.59060866755098,
2.59184744859274,2.59331024535127),.UNSPECIFIED.);
#1823=B_SPLINE_CURVE_WITH_KNOTS('',3,(#174099,#174100,#174101,#174102,#174103,
#174104,#174105,#174106,#174107,#174108,#174109,#174110,#174111,#174112,
#174113,#174114,#174115,#174116,#174117,#174118,#174119,#174120,#174121,
#174122,#174123,#174124,#174125,#174126,#174127,#174128,#174129,#174130,
#174131,#174132,#174133,#174134,#174135,#174136,#174137,#174138,#174139,
#174140,#174141,#174142,#174143,#174144,#174145,#174146,#174147,#174148,
#174149,#174150,#174151,#174152,#174153,#174154,#174155,#174156,#174157,
#174158,#174159,#174160,#174161,#174162,#174163,#174164,#174165,#174166,
#174167,#174168,#174169,#174170,#174171,#174172,#174173,#174174,#174175,
#174176,#174177,#174178,#174179,#174180,#174181,#174182,#174183,#174184,
#174185,#174186,#174187,#174188,#174189,#174190,#174191,#174192,#174193,
#174194,#174195,#174196,#174197,#174198,#174199,#174200,#174201,#174202,
#174203,#174204,#174205,#174206,#174207,#174208,#174209,#174210,#174211,
#174212,#174213,#174214,#174215,#174216,#174217,#174218,#174219,#174220,
#174221,#174222,#174223,#174224,#174225,#174226,#174227,#174228,#174229,
#174230,#174231,#174232,#174233,#174234,#174235,#174236,#174237,#174238,
#174239,#174240,#174241,#174242,#174243,#174244,#174245,#174246,#174247,
#174248,#174249,#174250,#174251,#174252,#174253,#174254,#174255,#174256,
#174257,#174258,#174259,#174260,#174261,#174262,#174263,#174264,#174265,
#174266,#174267,#174268,#174269,#174270,#174271,#174272,#174273,#174274,
#174275,#174276),.UNSPECIFIED.,.F.,.F.,(4,3,3,3,3,3,3,3,3,3,3,3,3,3,3,3,
3,3,3,3,3,3,3,3,3,3,3,3,3,3,3,3,3,3,3,3,3,3,3,3,3,3,3,3,3,3,3,3,3,3,3,3,
3,3,3,3,3,3,3,4),(-54.1065214908593,-53.9371682979412,-53.8337735608932,
-53.7305322787782,-53.6274123133858,-53.5243577451769,-53.4213345368191,
-53.3183086941465,-53.2151759273684,-53.1119868359585,-53.0086148425768,
-52.9383318479794,-52.8349371109315,-52.7316958288166,-52.6285758634243,
-52.5255212952155,-52.4224980868578,-52.3194722441853,-52.2163394774072,
-52.1131503859974,-52.0097783926158,-51.9394953980175,-51.8361006609695,
-51.7328593788545,-51.6297394134622,-51.5266848452533,-51.4236616368955,
-51.320635794223,-51.2175030274449,-51.114313936035,-51.0109419426534,-50.9406589480556,
-50.8372642110077,-50.7340229288926,-50.6309029635004,-50.5278483952914,
-50.4248251869337,-50.3217993442612,-50.2186665774831,-50.1154774860733,
-50.0121054926917,-49.9418224980937,-49.8384277610458,-49.7351864789308,
-49.6320665135385,-49.5290119453296,-49.4259887369719,-49.3229628942994,
-49.2198301275214,-49.1166410361116,-49.01326904273,-48.9429860481318,-48.8396205066959,
-48.7363953136968,-48.6332762150919,-48.5302290794622,-48.4271932051556,
-48.3241646395681,-48.2210652727541,-48.174029021668),.UNSPECIFIED.);
#1824=B_SPLINE_CURVE_WITH_KNOTS('',3,(#174277,#174278,#174279,#174280),
 .UNSPECIFIED.,.F.,.F.,(4,4),(-54.456513037791,-54.1065275196808),
 .UNSPECIFIED.);
#1825=B_SPLINE_CURVE_WITH_KNOTS('',3,(#174286,#174287,#174288,#174289,#174290,
#174291,#174292,#174293,#174294,#174295,#174296,#174297,#174298,#174299,
#174300,#174301,#174302,#174303,#174304,#174305),.UNSPECIFIED.,.F.,.F.,
(4,2,2,2,2,2,2,2,2,4),(2.59308993462329,2.59881536461045,2.60307197546038,
2.6056017133623,2.60754019170769,2.60961752672368,2.61288588653771,2.61668873260866,
2.62395258021943,2.66757550776084),.UNSPECIFIED.);
#1826=B_SPLINE_CURVE_WITH_KNOTS('',3,(#174306,#174307,#174308,#174309,#174310,
#174311,#174312,#174313,#174314,#174315,#174316,#174317,#174318,#174319,
#174320,#174321,#174322,#174323,#174324,#174325,#174326,#174327,#174328,
#174329,#174330,#174331,#174332,#174333,#174334,#174335,#174336,#174337,
#174338,#174339,#174340,#174341,#174342,#174343,#174344,#174345,#174346,
#174347,#174348,#174349,#174350,#174351,#174352,#174353,#174354,#174355,
#174356,#174357,#174358,#174359,#174360,#174361,#174362,#174363,#174364,
#174365,#174366,#174367,#174368,#174369,#174370,#174371,#174372,#174373,
#174374,#174375,#174376,#174377,#174378,#174379,#174380,#174381,#174382,
#174383,#174384,#174385,#174386,#174387,#174388,#174389,#174390,#174391,
#174392,#174393,#174394,#174395,#174396,#174397,#174398,#174399,#174400,
#174401,#174402,#174403,#174404,#174405,#174406,#174407,#174408,#174409,
#174410,#174411,#174412,#174413,#174414,#174415,#174416,#174417,#174418,
#174419,#174420,#174421,#174422,#174423,#174424,#174425,#174426,#174427,
#174428,#174429,#174430,#174431,#174432,#174433,#174434,#174435,#174436,
#174437,#174438,#174439,#174440,#174441,#174442,#174443,#174444,#174445,
#174446,#174447,#174448,#174449,#174450,#174451,#174452,#174453,#174454,
#174455,#174456,#174457,#174458,#174459,#174460,#174461,#174462,#174463,
#174464,#174465,#174466,#174467,#174468,#174469,#174470,#174471,#174472,
#174473,#174474,#174475,#174476,#174477,#174478,#174479,#174480,#174481,
#174482,#174483,#174484,#174485,#174486,#174487,#174488,#174489,#174490,
#174491,#174492,#174493,#174494,#174495,#174496,#174497,#174498,#174499,
#174500,#174501,#174502,#174503,#174504,#174505,#174506,#174507,#174508,
#174509,#174510,#174511,#174512,#174513,#174514,#174515,#174516,#174517,
#174518,#174519),.UNSPECIFIED.,.F.,.F.,(4,2,2,2,2,2,2,2,2,2,2,2,2,2,2,2,
2,2,2,2,2,2,2,2,2,2,2,2,2,2,2,2,2,2,2,2,2,2,2,2,2,2,2,2,2,2,2,2,2,2,2,2,
2,2,2,2,2,2,2,2,2,2,2,2,2,2,2,2,2,2,2,2,2,2,2,2,2,2,2,2,2,2,2,2,2,2,2,2,
2,2,2,2,2,2,2,2,2,2,2,2,2,2,2,2,2,2,4),(0.000649993331013773,0.0375152736453762,
0.0412926066958227,0.0433020341715962,0.044607215832664,0.045844419448192,
0.0469177320618385,0.0482917912985203,0.0511320599888608,0.0879797115895702,
0.109399218190971,0.136182458586284,0.146436099124581,0.149706960391475,
0.151785049252133,0.153723648856619,0.15625271235973,0.160506368957157,
0.193188856063357,0.222561137876658,0.244175532207324,0.254295403786826,
0.25648530331634,0.257733434758561,0.258805438493602,0.260163923762618,
0.262836090595815,0.280220127817376,0.329263705439906,0.347305789337896,
0.354573683519191,0.36000255078723,0.362567762856761,0.364505099941212,
0.366333302380224,0.368881421716173,0.375563408649001,0.430966318990965,
0.45531833772441,0.466218362236338,0.468466827385657,0.469717966669812,
0.470789714733089,0.472144237015971,0.474885954457074,0.493328404523347,
0.537460304227698,0.56533181314619,0.571665318741461,0.574356955714583,
0.57631551717809,0.578111655021596,0.580996197394739,0.587999833063062,
0.639384728107681,0.6665155305315,0.678128415364886,0.680418166758709,0.681678306830284,
0.682749311508137,0.684092164238236,0.686691256343921,0.702216945856713,
0.708760927231134,0.722633874188153,0.755493937891593,0.772056441017398,
0.782367865525588,0.785616669809531,0.787690051800405,0.789630786629262,
0.792172032044759,0.796467187329842,0.831578300272903,0.880465436321519,
0.89028861056827,0.892468467938671,0.893704699529089,0.894778400789985,
0.896154565678567,0.899004695521442,0.935374552606732,0.989163011369373,
0.995619065943052,0.998331634006407,1.00029412823005,1.0020861016653,1.00494702788069,
1.01180630602425,1.06524491368085,1.09093515786658,1.10218655441291,1.10445597198694,
1.10571178057254,1.10678326518238,1.10813201829251,1.11075808370708,1.12692227782077,
1.1775802709192,1.20199423988746,1.20789425851965,1.21051032259266,1.21245602088232,
1.21427041747359,1.21676502677054,1.2231148737998,1.25968337114772),
 .UNSPECIFIED.);
#1827=B_SPLINE_CURVE_WITH_KNOTS('',3,(#174521,#174522,#174523,#174524,#174525,
#174526,#174527,#174528,#174529,#174530),.UNSPECIFIED.,.F.,.F.,(4,1,1,1,
1,1,1,4),(-60.3897037700498,-59.9301869977125,-58.9313505477506,-57.9325140977887,
-56.9336776478269,-55.934841197865,-54.9360047479031,-54.456513037791),
 .UNSPECIFIED.);
#1828=B_SPLINE_CURVE_WITH_KNOTS('',3,(#174531,#174532,#174533,#174534,#174535,
#174536,#174537,#174538,#174539,#174540,#174541,#174542,#174543,#174544,
#174545,#174546,#174547,#174548),.UNSPECIFIED.,.F.,.F.,(4,2,2,2,2,2,2,2,
4),(0.000658789710875621,0.0033297019558972,0.00592165925672697,0.00778879716285326,
0.00964368964991593,0.0114909186466428,0.0146445374956457,0.0233614961612485,
0.0750732887615297),.UNSPECIFIED.);
#1829=B_SPLINE_CURVE_WITH_KNOTS('',3,(#174553,#174554,#174555,#174556,#174557,
#174558,#174559,#174560,#174561,#174562,#174563,#174564,#174565,#174566,
#174567,#174568,#174569,#174570,#174571,#174572,#174573,#174574,#174575,
#174576,#174577,#174578,#174579,#174580,#174581,#174582,#174583,#174584,
#174585,#174586,#174587,#174588,#174589,#174590,#174591,#174592,#174593,
#174594,#174595,#174596,#174597,#174598,#174599,#174600,#174601,#174602,
#174603,#174604,#174605,#174606,#174607,#174608,#174609,#174610,#174611,
#174612,#174613,#174614,#174615,#174616,#174617,#174618,#174619,#174620,
#174621,#174622,#174623,#174624,#174625,#174626,#174627,#174628,#174629,
#174630,#174631,#174632,#174633,#174634,#174635,#174636,#174637,#174638,
#174639,#174640,#174641,#174642,#174643,#174644,#174645,#174646,#174647,
#174648,#174649,#174650,#174651,#174652,#174653,#174654,#174655,#174656,
#174657,#174658,#174659,#174660,#174661,#174662,#174663,#174664,#174665,
#174666,#174667,#174668,#174669,#174670,#174671,#174672,#174673,#174674,
#174675,#174676,#174677,#174678,#174679,#174680,#174681,#174682,#174683,
#174684,#174685,#174686,#174687,#174688,#174689,#174690,#174691,#174692,
#174693,#174694,#174695,#174696,#174697,#174698,#174699,#174700,#174701,
#174702,#174703,#174704,#174705,#174706,#174707,#174708,#174709,#174710,
#174711,#174712,#174713,#174714,#174715,#174716,#174717,#174718,#174719,
#174720,#174721,#174722,#174723,#174724,#174725,#174726,#174727,#174728,
#174729,#174730,#174731,#174732,#174733,#174734,#174735,#174736,#174737,
#174738,#174739,#174740,#174741,#174742,#174743,#174744,#174745,#174746,
#174747,#174748,#174749,#174750,#174751,#174752,#174753,#174754,#174755,
#174756,#174757,#174758,#174759,#174760,#174761,#174762,#174763,#174764,
#174765,#174766,#174767,#174768,#174769,#174770,#174771,#174772,#174773,
#174774),.UNSPECIFIED.,.F.,.F.,(4,2,2,2,2,2,2,2,2,2,2,2,2,2,2,2,2,2,2,2,
2,2,2,2,2,2,2,2,2,2,2,2,2,2,2,2,2,2,2,2,2,2,2,2,2,2,2,2,2,2,2,2,2,2,2,2,
2,2,2,2,2,2,2,2,2,2,2,2,2,2,2,2,2,2,2,2,2,2,2,2,2,2,2,2,2,2,2,2,2,2,2,2,
2,2,2,2,2,2,2,2,2,2,2,2,2,2,2,2,2,2,4),(1.2598188162962,1.28582910675168,
1.32659483739134,1.33166075036229,1.33412021359612,1.3360430637854,1.33817454540318,
1.34168704094204,1.35456214699032,1.3772629349575,1.41585039442087,1.42084455493994,
1.43685065379829,1.43946985762439,1.44081696261975,1.44188812356032,1.44314470097155,
1.44541841322834,1.45675099277767,1.48276037789335,1.53567697460108,1.54257189724511,
1.54543830941899,1.54723100415685,1.5491921112309,1.55189875997267,1.55832172771228,
1.58694418749935,1.63822339094734,1.64928405207265,1.65143088219273,1.65278721060316,
1.65385904268073,1.6551087399456,1.65735075673663,1.66814586155088,1.69210600879927,
1.74805395327426,1.75467916201693,1.757218341053,1.75904412504075,1.76098257635116,
1.76355551061247,1.76921953544927,1.79185998894947,1.82467505848605,1.82892885538883,
1.86039079648171,1.86330220822099,1.8646901279052,1.86576474414343,1.86699278994439,
1.86913638286826,1.87844769522067,1.92759244244472,1.96295371463675,1.96725087208344,
1.9697924031215,1.97173282764153,1.97380536503933,1.97705177386893,1.98734648215883,
2.00387577778063,2.03673167692832,2.04840959727023,2.05699946981549,2.0727344762376,
2.07534606040473,2.0766914290874,2.07776236004584,2.07902000308596,2.08129904606364,
2.09272854401299,2.11912362483884,2.1714800090376,2.17841409126171,2.18128674014139,
2.18308041658102,2.18504025736265,2.18774087743751,2.19412935638219,2.23964987147934,
2.28171599859575,2.28636347950216,2.28809332059615,2.28911643491209,2.29020986610841,
2.29172761090144,2.29535521465203,2.30046057235922,2.31460692435585,2.36435596823844,
2.37360623771747,2.38839293755108,2.39219622620605,2.39441418037008,2.39632549683361,
2.39865498519619,2.40308089724313,2.42536046955279,2.46852771658149,2.4962144512301,
2.49912046666446,2.50050729541288,2.5015817501905,2.50281037630488,2.50410337152851,
2.50876349509607,2.53287928142517,2.55377715173552,2.59308993462329),
 .UNSPECIFIED.);
#1830=B_SPLINE_CURVE_WITH_KNOTS('',3,(#174775,#174776,#174777,#174778,#174779,
#174780,#174781,#174782,#174783,#174784,#174785,#174786,#174787,#174788,
#174789,#174790,#174791,#174792,#174793,#174794,#174795,#174796,#174797,
#174798,#174799,#174800,#174801,#174802,#174803,#174804,#174805,#174806,
#174807,#174808,#174809,#174810,#174811,#174812,#174813,#174814,#174815,
#174816,#174817,#174818,#174819,#174820,#174821,#174822,#174823,#174824,
#174825,#174826,#174827,#174828,#174829,#174830,#174831,#174832,#174833,
#174834,#174835,#174836,#174837,#174838,#174839,#174840,#174841,#174842,
#174843,#174844,#174845,#174846,#174847,#174848,#174849,#174850,#174851,
#174852,#174853,#174854,#174855,#174856,#174857,#174858,#174859,#174860,
#174861,#174862,#174863,#174864,#174865,#174866,#174867,#174868,#174869,
#174870,#174871,#174872,#174873,#174874,#174875,#174876,#174877,#174878,
#174879,#174880,#174881,#174882,#174883,#174884,#174885,#174886,#174887,
#174888,#174889,#174890,#174891,#174892,#174893,#174894,#174895,#174896,
#174897,#174898,#174899,#174900,#174901,#174902,#174903,#174904,#174905,
#174906,#174907,#174908,#174909,#174910,#174911,#174912,#174913,#174914,
#174915,#174916,#174917,#174918,#174919,#174920,#174921,#174922,#174923,
#174924,#174925,#174926,#174927,#174928,#174929,#174930,#174931,#174932,
#174933,#174934,#174935,#174936,#174937,#174938,#174939,#174940,#174941,
#174942,#174943,#174944,#174945,#174946,#174947,#174948,#174949,#174950,
#174951,#174952,#174953,#174954,#174955,#174956,#174957,#174958,#174959,
#174960,#174961,#174962,#174963,#174964,#174965,#174966,#174967,#174968,
#174969,#174970,#174971,#174972,#174973,#174974,#174975,#174976,#174977,
#174978,#174979,#174980,#174981,#174982,#174983,#174984,#174985,#174986,
#174987,#174988,#174989,#174990,#174991,#174992,#174993,#174994,#174995,
#174996,#174997,#174998,#174999,#175000,#175001,#175002,#175003,#175004,
#175005,#175006),.UNSPECIFIED.,.F.,.F.,(4,2,2,2,2,2,2,2,2,2,2,2,2,2,2,2,
2,2,2,2,2,2,2,2,2,2,2,2,2,2,2,2,2,2,2,2,2,2,2,2,2,2,2,2,2,2,2,2,2,2,2,2,
2,2,2,2,2,2,2,2,2,2,2,2,2,2,2,2,2,2,2,2,2,2,2,2,2,2,2,2,2,2,2,2,2,2,2,2,
2,2,2,2,2,2,2,2,2,2,2,2,2,2,2,2,2,2,2,2,2,2,2,2,2,2,2,4),(0.0750732887615297,
0.0895786872185756,0.108776673444175,0.112687667588427,0.114252339386623,
0.115354626383585,0.116366707255712,0.118038562888942,0.122314119578349,
0.178030895777346,0.209836521089513,0.214455835189256,0.21722182163431,
0.219725106281578,0.221625903726026,0.223450329915231,0.225983634845776,
0.232570915468512,0.288908008162023,0.312655305002868,0.323392618135194,
0.325631403689644,0.326880523911942,0.327952621545743,0.329310255392404,
0.331977827467359,0.349225793650038,0.365434006915295,0.40026058837796,
0.423361560096201,0.42908852568208,0.431673378061521,0.433614092718227,
0.435437105598377,0.437964605124127,0.444513982543606,0.501229072546634,
0.524735771556337,0.535407711707381,0.537642637038817,0.538890990233706,
0.539963288418181,0.541322280536716,0.543995847386938,0.561403803782938,
0.611255794604785,0.635241862161705,0.641086203964012,0.643692398004577,
0.645636600712106,0.647453819283593,0.649958945237493,0.656371159543673,
0.714276531250413,0.73703090948458,0.747494158372973,0.749716141419215,
0.750961706070528,0.752034375427397,0.753397406368537,0.756089736758378,
0.774034475163358,0.822088316566691,0.840408384767806,0.851497265122604,
0.854832750834517,0.856925471406221,0.85885961686657,0.861357330377948,
0.865502438252775,0.893394867270794,0.947161446532259,0.959371234235877,
0.961693681471469,0.962961127490909,0.964031989213525,0.965366667202426,
0.967441902861164,0.977393962372905,0.983033419115146,0.992434620947976,
1.00400487314063,1.03685416617455,1.05339653638974,1.06369972440442,1.06694822242758,
1.06902195931009,1.07096341303229,1.07350615789104,1.07780509881571,1.11311795905019,
1.16237601762062,1.17171435900122,1.17386077287483,1.17508987724573,1.17616506193869,
1.17755323318852,1.18046348893946,1.20859690640356,1.2482888946344,1.26523562654097,
1.27572113131065,1.27899060545621,1.28106906901157,1.28300889420011,1.28554081197511,
1.28980206145261,1.33480531537179,1.37985976923109,1.3845853353168,1.38632777019847,
1.3873538428049,1.38844662397774,1.38995724915956,1.393539137418,1.40896669254699),
 .UNSPECIFIED.);
#1831=B_SPLINE_CURVE_WITH_KNOTS('',3,(#175012,#175013,#175014,#175015,#175016),
 .UNSPECIFIED.,.F.,.F.,(4,1,4),(76.7075601022117,76.9104066470643,77.0584303716429),
 .UNSPECIFIED.);
#1832=B_SPLINE_CURVE_WITH_KNOTS('',3,(#175017,#175018,#175019,#175020,#175021,
#175022,#175023,#175024,#175025,#175026,#175027,#175028,#175029,#175030,
#175031,#175032,#175033,#175034,#175035,#175036,#175037,#175038,#175039,
#175040,#175041,#175042,#175043,#175044,#175045,#175046,#175047,#175048,
#175049,#175050,#175051,#175052,#175053,#175054,#175055,#175056,#175057,
#175058,#175059,#175060,#175061,#175062,#175063,#175064,#175065,#175066,
#175067,#175068,#175069,#175070,#175071,#175072,#175073,#175074,#175075,
#175076,#175077,#175078,#175079,#175080,#175081,#175082,#175083,#175084,
#175085,#175086,#175087,#175088,#175089,#175090,#175091,#175092,#175093,
#175094,#175095,#175096,#175097,#175098,#175099,#175100,#175101,#175102,
#175103,#175104,#175105,#175106,#175107,#175108,#175109,#175110,#175111,
#175112,#175113,#175114,#175115,#175116,#175117,#175118,#175119,#175120,
#175121,#175122,#175123,#175124,#175125,#175126,#175127,#175128,#175129,
#175130,#175131,#175132,#175133,#175134,#175135,#175136,#175137,#175138,
#175139,#175140,#175141,#175142,#175143,#175144,#175145,#175146,#175147,
#175148,#175149,#175150,#175151,#175152,#175153,#175154,#175155,#175156,
#175157,#175158,#175159,#175160,#175161,#175162,#175163,#175164,#175165,
#175166,#175167,#175168,#175169,#175170,#175171,#175172,#175173,#175174,
#175175,#175176,#175177,#175178,#175179,#175180,#175181,#175182,#175183,
#175184,#175185,#175186,#175187,#175188,#175189,#175190,#175191,#175192,
#175193,#175194,#175195,#175196,#175197,#175198,#175199,#175200,#175201,
#175202,#175203,#175204,#175205,#175206,#175207,#175208,#175209,#175210,
#175211,#175212,#175213,#175214,#175215,#175216,#175217,#175218,#175219,
#175220,#175221,#175222,#175223,#175224,#175225,#175226,#175227,#175228,
#175229,#175230,#175231,#175232,#175233,#175234,#175235,#175236,#175237,
#175238),.UNSPECIFIED.,.F.,.F.,(4,2,2,2,2,2,2,2,2,2,2,2,2,2,2,2,2,2,2,2,
2,2,2,2,2,2,2,2,2,2,2,2,2,2,2,2,2,2,2,2,2,2,2,2,2,2,2,2,2,2,2,2,2,2,2,2,
2,2,2,2,2,2,2,2,2,2,2,2,2,2,2,2,2,2,2,2,2,2,2,2,2,2,2,2,2,2,2,2,2,2,2,2,
2,2,2,2,2,2,2,2,2,2,2,2,2,2,2,2,2,2,4),(0.00062922477804048,0.0464652953959511,
0.0539874627083681,0.0578868262224725,0.0612218917618552,0.0633140104223921,
0.0652473689506565,0.0677437427811126,0.0718859251347045,0.0997158380709969,
0.113763875467969,0.12930975099674,0.154610309606332,0.165743607840038,
0.168012355284411,0.16926952399704,0.170340543990751,0.171686645238151,
0.174301472994702,0.190228702005755,0.195859651481846,0.25279017795695,
0.268941263732326,0.272736315114818,0.274930060881375,0.276843183245678,
0.279203796669903,0.282810236411761,0.299521474717382,0.307016312503351,
0.35552052635381,0.370248070400744,0.378141297512718,0.380172947110739,
0.381376133496349,0.382455933488197,0.383862893393866,0.386229424307423,
0.40165571259872,0.405922318104049,0.448896606019998,0.47682861694909,0.483168954246668,
0.485861489510229,0.487819967755852,0.489615518845367,0.492497998416956,
0.499490908048754,0.551011590897581,0.578035038566169,0.58962067389478,
0.591908636141562,0.59316826235519,0.594239113763674,0.595582133715924,
0.598182596225254,0.613747895324114,0.620206829222099,0.661617384913786,
0.68888713635835,0.695146982192309,0.697825810435743,0.699781913499077,
0.70158057463847,0.704479716433519,0.711572252189626,0.761225744758292,
0.799536004107826,0.803140089386526,0.804653944556405,0.805746779238389,
0.806771088843483,0.808506669136336,0.81319120071484,0.854270650314107,
0.90069679167419,0.907088247212731,0.909789580758431,0.911749742973229,
0.913543582016164,0.916416192282476,0.923348618781982,0.975791660662828,
1.00216367739533,1.01358740277245,1.01586636896956,1.01712409769934,1.01819518257729,
1.01954084145329,1.02215327420812,1.03800352486472,1.04274687359478,1.05802403925964,
1.09089716689076,1.10747761982684,1.1177968934593,1.12104640234922,1.12311980943024,
1.12506026959418,1.12760072530062,1.13189358223016,1.17429083615549,1.20334618781477,
1.22296071006421,1.22691560694454,1.22848716391289,1.22959066388589,1.23060105632183,
1.23226455229217,1.23648935279628,1.2598188162962),.UNSPECIFIED.);
#1833=B_SPLINE_CURVE_WITH_KNOTS('',3,(#175240,#175241,#175242,#175243,#175244,
#175245,#175246,#175247,#175248,#175249,#175250,#175251,#175252,#175253,
#175254,#175255,#175256,#175257,#175258,#175259,#175260,#175261,#175262,
#175263,#175264,#175265,#175266,#175267,#175268,#175269,#175270,#175271,
#175272,#175273,#175274,#175275,#175276,#175277,#175278,#175279,#175280,
#175281,#175282,#175283,#175284,#175285,#175286,#175287,#175288,#175289,
#175290,#175291,#175292,#175293,#175294,#175295,#175296,#175297,#175298,
#175299,#175300,#175301,#175302,#175303,#175304,#175305,#175306,#175307,
#175308,#175309,#175310,#175311,#175312,#175313,#175314,#175315,#175316,
#175317,#175318,#175319,#175320,#175321,#175322,#175323,#175324,#175325,
#175326,#175327,#175328,#175329,#175330,#175331,#175332,#175333,#175334,
#175335,#175336,#175337,#175338,#175339,#175340,#175341,#175342,#175343,
#175344,#175345,#175346,#175347,#175348,#175349,#175350,#175351,#175352,
#175353,#175354,#175355,#175356,#175357,#175358,#175359,#175360,#175361,
#175362,#175363,#175364,#175365,#175366,#175367,#175368,#175369,#175370,
#175371,#175372,#175373,#175374,#175375,#175376,#175377,#175378,#175379,
#175380,#175381,#175382,#175383,#175384,#175385,#175386,#175387,#175388,
#175389,#175390,#175391,#175392,#175393,#175394,#175395,#175396,#175397,
#175398,#175399,#175400,#175401,#175402,#175403,#175404,#175405,#175406,
#175407,#175408,#175409,#175410,#175411,#175412,#175413,#175414,#175415,
#175416,#175417,#175418,#175419,#175420,#175421,#175422,#175423,#175424,
#175425,#175426,#175427,#175428,#175429,#175430,#175431,#175432,#175433,
#175434,#175435,#175436,#175437,#175438,#175439,#175440,#175441,#175442,
#175443,#175444,#175445,#175446,#175447,#175448,#175449,#175450,#175451,
#175452,#175453,#175454,#175455,#175456,#175457,#175458,#175459,#175460,
#175461,#175462,#175463),.UNSPECIFIED.,.F.,.F.,(4,2,2,2,2,2,2,2,2,2,2,2,
2,2,2,2,2,2,2,2,2,2,2,2,2,2,2,2,2,2,2,2,2,2,2,2,2,2,2,2,2,2,2,2,2,2,2,2,
2,2,2,2,2,2,2,2,2,2,2,2,2,2,2,2,2,2,2,2,2,2,2,2,2,2,2,2,2,2,2,2,2,2,2,2,
2,2,2,2,2,2,2,2,2,2,2,2,2,2,2,2,2,2,2,2,2,2,2,2,2,2,2,4),(1.40896669254699,
1.43117951109762,1.48160626610979,1.48866533053147,1.49155996689647,1.49335859904134,
1.49531687243928,1.49800265062375,1.50429705257051,1.53183798945899,1.56024380039991,
1.58257536586916,1.59528320803545,1.59752392806156,1.59890907121816,1.59998396177195,
1.60121503985215,1.60337032463693,1.61283263139795,1.66202152608611,1.69722883918779,
1.70152641174088,1.70406884250338,1.70601033064397,1.7080843692321,1.7113338917161,
1.72164489299814,1.73820645258912,1.77110067801436,1.78483636905165,1.79171010539514,
1.79192676507287,1.79545007095206,1.80740666043681,1.80960671783378,1.81097953665053,
1.81205317446822,1.81329222802112,1.81548402248912,1.8254790104123,1.87421219717204,
1.90927148237337,1.91356683841726,1.91610853538612,1.9180497958077,1.92012391368317,
1.92337423396291,1.93369344624765,1.95027360004668,1.98318193416041,1.99836891046661,
2.00321053728236,2.01910159076681,2.02171603681438,2.02306243915953,2.02413396056373,
2.02539202732717,2.02767115058287,2.03908677452003,2.06541657067306,2.11791275224925,
2.12484308668044,2.12771603955699,2.12951044785643,2.13147152279433,2.13417463793488,
2.14057275843119,2.18836823029259,2.22807348290449,2.23281799553136,2.23456311481422,
2.23558958703295,2.23668179567086,2.23819000446309,2.24175873064458,2.2794736160787,
2.3298223184813,2.33688357635813,2.33977825869028,2.34157666324293,2.343534485416,
2.34621927628665,2.35250966335699,2.38002215823233,2.42191963479165,2.44297304607341,
2.44578939258029,2.44715905382501,2.44819622862635,2.44939626614753,2.45067690309327,
2.4526266300887,2.45624584904207,2.46485966520697,2.49773269375569,2.54162822662122,
2.54885151925285,2.55177335728039,2.55357676114043,2.55553068334886,2.55819334626703,
2.56435560956493,2.59082877988912,2.6483497821524,2.65622246182487,2.65831873378907,
2.65954887037209,2.66060581764147,2.66165184919058,2.66300245522682,2.66546082872914,
2.66855489445154),.UNSPECIFIED.);
#1834=B_SPLINE_CURVE_WITH_KNOTS('',3,(#175464,#175465,#175466,#175467,#175468,
#175469),.UNSPECIFIED.,.F.,.F.,(4,2,4),(0.000817337805837695,0.0612255019915846,
0.0752219354471869),.UNSPECIFIED.);
#1835=B_SPLINE_CURVE_WITH_KNOTS('',3,(#175475,#175476,#175477,#175478,#175479,
#175480,#175481,#175482,#175483,#175484,#175485,#175486,#175487),
 .UNSPECIFIED.,.F.,.F.,(4,3,3,3,4),(82.9907456874198,83.0928761471997,83.1948834239681,
83.2967928188084,83.3413404231495),.UNSPECIFIED.);
#1836=B_SPLINE_CURVE_WITH_KNOTS('',3,(#175488,#175489,#175490,#175491,#175492,
#175493,#175494,#175495,#175496,#175497),.UNSPECIFIED.,.F.,.F.,(4,1,1,1,
1,1,1,4),(77.0584303716429,77.9092430970262,78.9080795469881,79.90691599695,
80.9057524469118,81.9045888968737,82.9034253468356,82.9907454093913),
 .UNSPECIFIED.);
#1837=B_SPLINE_CURVE_WITH_KNOTS('',3,(#175498,#175499,#175500,#175501,#175502,
#175503,#175504,#175505,#175506,#175507,#175508,#175509,#175510,#175511,
#175512,#175513,#175514,#175515,#175516,#175517,#175518,#175519,#175520,
#175521,#175522,#175523,#175524,#175525,#175526,#175527,#175528,#175529,
#175530,#175531,#175532,#175533,#175534,#175535,#175536,#175537,#175538,
#175539,#175540,#175541,#175542,#175543,#175544,#175545,#175546,#175547,
#175548,#175549,#175550,#175551,#175552,#175553,#175554,#175555,#175556,
#175557,#175558,#175559,#175560,#175561,#175562,#175563,#175564,#175565,
#175566,#175567,#175568,#175569,#175570,#175571,#175572,#175573,#175574,
#175575,#175576,#175577,#175578,#175579,#175580,#175581,#175582,#175583,
#175584,#175585,#175586,#175587,#175588,#175589,#175590,#175591,#175592,
#175593,#175594,#175595,#175596,#175597,#175598,#175599,#175600,#175601,
#175602,#175603,#175604,#175605,#175606,#175607,#175608,#175609,#175610,
#175611,#175612,#175613,#175614,#175615,#175616,#175617,#175618,#175619,
#175620,#175621,#175622,#175623,#175624,#175625,#175626,#175627,#175628,
#175629,#175630,#175631,#175632,#175633,#175634,#175635,#175636,#175637,
#175638,#175639,#175640,#175641,#175642,#175643,#175644,#175645,#175646,
#175647,#175648,#175649,#175650,#175651,#175652,#175653,#175654,#175655,
#175656,#175657,#175658,#175659,#175660,#175661,#175662,#175663,#175664,
#175665,#175666,#175667,#175668,#175669,#175670,#175671,#175672,#175673,
#175674,#175675,#175676,#175677,#175678,#175679,#175680,#175681,#175682,
#175683,#175684,#175685,#175686,#175687,#175688,#175689,#175690,#175691,
#175692,#175693,#175694,#175695,#175696,#175697,#175698,#175699,#175700,
#175701,#175702,#175703,#175704,#175705,#175706,#175707,#175708,#175709,
#175710,#175711,#175712,#175713,#175714,#175715,#175716,#175717,#175718,
#175719,#175720,#175721,#175722,#175723,#175724,#175725,#175726,#175727,
#175728,#175729,#175730,#175731,#175732,#175733,#175734,#175735,#175736,
#175737,#175738,#175739,#175740,#175741,#175742,#175743,#175744,#175745,
#175746,#175747,#175748,#175749,#175750,#175751,#175752,#175753,#175754,
#175755,#175756,#175757,#175758,#175759,#175760,#175761,#175762,#175763,
#175764,#175765,#175766,#175767,#175768,#175769),.UNSPECIFIED.,.F.,.F.,
(4,2,2,2,2,2,2,2,2,2,2,2,2,2,2,2,2,2,2,2,2,2,2,2,2,2,2,2,2,2,2,2,2,2,2,
2,2,2,2,2,2,2,2,2,2,2,2,2,2,2,2,2,2,2,2,2,2,2,2,2,2,2,2,2,2,2,2,2,2,2,2,
2,2,2,2,2,2,2,2,2,2,2,2,2,2,2,2,2,2,2,2,2,2,2,2,2,2,2,2,2,2,2,2,2,2,2,2,
2,2,2,2,2,2,2,2,2,2,2,2,2,2,2,2,2,2,2,2,2,2,2,2,2,2,2,2,4),(0.0752219354471869,
0.0876737803832443,0.0938318759611345,0.096492981468071,0.0984458548715177,
0.100248360755656,0.103168888387438,0.110389690462612,0.15424713468251,
0.195394582587352,0.199212958657244,0.201237805204114,0.202549338024773,
0.203772973796596,0.20377654050265,0.203780119950459,0.203783712088444,
0.203787549478355,0.203791448764298,0.203795411146991,0.203799437954619,
0.203803530609202,0.203807690589143,0.203811919370073,0.20381621842432,
0.203820589227681,0.203825033406919,0.203829552627674,0.203834148630411,
0.203838823136086,0.203843577879537,0.203848414698621,0.2048921653215,0.206274877504582,
0.209159635945463,0.243336900398366,0.277589533678257,0.294133556780751,
0.304436070586588,0.307683448565633,0.309756252284464,0.311696679080571,
0.314237857731063,0.318533654699075,0.353751370195098,0.402995139423211,
0.412389257103734,0.414538925950045,0.415768366383412,0.416842851758761,
0.41822881172915,0.421129832178343,0.453737204220591,0.489082677107781,
0.512192572655288,0.517920263062228,0.520504973984694,0.522445393980685,
0.524267992549417,0.526794698530033,0.533340773146543,0.590075625735493,
0.613557703932693,0.624222135448335,0.626456317732056,0.627704373743318,
0.628776489699957,0.63013534480763,0.632808925340623,0.650227404118175,
0.698915143009477,0.717170928764429,0.728231285602008,0.731563210335695,
0.733654829485937,0.735588730006404,0.738087212264651,0.742235953847532,
0.770296111813773,0.823884046818624,0.836075479382837,0.838396573882568,
0.839663549231086,0.840734171725199,0.842068750797324,0.844144192816116,
0.854103858557716,0.859578958206535,0.86002731298575,0.86691547220709,0.880641619226851,
0.913502670778416,0.930064599266058,0.940375979427016,0.943624936420555,
0.945698455912095,0.947639347568836,0.950180838914409,0.95447650080002,
0.989603716312452,1.03853525985647,1.04831086776148,1.05048759969225,1.05172320234754,
1.05279708883849,1.05417444696276,1.05703033255149,1.07981224668153,1.09265615970665,
1.12551214073723,1.14206550455317,1.15237330951317,1.15562207539461,1.15769569773731,
1.15963684361155,1.16217889575568,1.16647601642632,1.20168366033932,1.25086614322686,
1.26035552064793,1.26251251995824,1.26374386128169,1.26481852327256,1.2662027589569,
1.26909333890624,1.29479692775303,1.33424453012331,1.36196857526904,1.36610927293393,
1.36860580503195,1.37053989936434,1.37263342460125,1.37597205063585,1.3870884923977,
1.4054744587401,1.40869684638067),.UNSPECIFIED.);
#1838=B_SPLINE_CURVE_WITH_KNOTS('',3,(#175775,#175776,#175777,#175778,#175779,
#175780,#175781,#175782,#175783,#175784,#175785,#175786,#175787,#175788,
#175789,#175790,#175791,#175792,#175793,#175794,#175795,#175796,#175797,
#175798,#175799,#175800),.UNSPECIFIED.,.F.,.F.,(4,2,2,2,2,2,2,2,2,2,2,2,
4),(2.59377040355344,2.61306920303431,2.62518493005823,2.62701213587885,
2.62801357239381,2.63670095557141,2.63985192811609,2.64169888631868,2.64355375008281,
2.64542171035433,2.64782304230046,2.65156277527943,2.66819514587953),
 .UNSPECIFIED.);
#1839=B_SPLINE_CURVE_WITH_KNOTS('',3,(#175801,#175802,#175803,#175804,#175805,
#175806,#175807,#175808,#175809,#175810,#175811,#175812,#175813,#175814,
#175815,#175816,#175817,#175818,#175819,#175820,#175821,#175822,#175823,
#175824,#175825,#175826,#175827,#175828,#175829,#175830,#175831,#175832,
#175833,#175834,#175835,#175836,#175837,#175838,#175839,#175840,#175841,
#175842,#175843,#175844,#175845,#175846,#175847,#175848,#175849,#175850,
#175851,#175852,#175853,#175854,#175855,#175856,#175857,#175858,#175859,
#175860,#175861,#175862,#175863,#175864,#175865,#175866,#175867,#175868,
#175869,#175870,#175871,#175872,#175873,#175874,#175875,#175876,#175877,
#175878,#175879,#175880,#175881,#175882,#175883,#175884,#175885,#175886,
#175887,#175888,#175889,#175890,#175891,#175892,#175893,#175894,#175895,
#175896,#175897,#175898,#175899,#175900,#175901,#175902,#175903,#175904,
#175905,#175906,#175907,#175908,#175909,#175910,#175911,#175912,#175913,
#175914,#175915,#175916,#175917,#175918,#175919,#175920,#175921,#175922,
#175923,#175924,#175925,#175926,#175927,#175928,#175929,#175930,#175931,
#175932,#175933,#175934,#175935,#175936,#175937,#175938,#175939,#175940,
#175941,#175942,#175943,#175944,#175945,#175946,#175947,#175948,#175949,
#175950,#175951,#175952,#175953,#175954,#175955,#175956,#175957,#175958,
#175959,#175960,#175961,#175962,#175963,#175964,#175965,#175966,#175967,
#175968,#175969,#175970,#175971,#175972,#175973,#175974,#175975,#175976,
#175977,#175978,#175979,#175980,#175981),.UNSPECIFIED.,.F.,.F.,(4,3,3,3,
3,3,3,3,3,3,3,3,3,3,3,3,3,3,3,3,3,3,3,3,3,3,3,3,3,3,3,3,3,3,3,3,3,3,3,3,
3,3,3,3,3,3,3,3,3,3,3,3,3,3,3,3,3,3,3,3,4),(83.3413404231495,83.4431911085275,
83.5450419932945,83.646994864468,83.7490046560777,83.8511878009641,83.9022617967974,
84.0056565338454,84.1088978159605,84.2120177813528,84.3150723495617,84.4180955579193,
84.5211214005918,84.6242541673699,84.7274432587796,84.8308152521613,84.9010982467593,
85.0044929838073,85.1077342659222,85.2108542313146,85.3139087995235,85.4169320078813,
85.5199578505539,85.623090617332,85.7262797087419,85.8296517021236,85.8999346967212,
86.0033294337692,86.1065707158841,86.2096906812764,86.3127452494854,86.4157684578432,
86.5187943005158,86.6219270672939,86.7251161587037,86.8284881520853,86.8987711466831,
87.0021658837311,87.105407165846,87.2085271312384,87.3115816994473,87.4146049078052,
87.517630750478,87.620763517256,87.7239526086658,87.8273246020474,87.897607596645,
88.0010023336928,88.1042436158078,88.2073635812001,88.3104181494088,88.4134413577666,
88.5164672004389,88.6195999672169,88.7227890586268,88.8261610520084,88.8964440466068,
89.0132269961626,89.1295586830744,89.2451399878363,89.2739307161836),
 .UNSPECIFIED.);
#1840=B_SPLINE_CURVE_WITH_KNOTS('',3,(#175983,#175984,#175985,#175986,#175987,
#175988,#175989,#175990,#175991,#175992,#175993,#175994,#175995,#175996,
#175997,#175998,#175999,#176000,#176001,#176002,#176003,#176004,#176005,
#176006,#176007,#176008,#176009,#176010,#176011,#176012,#176013,#176014,
#176015,#176016,#176017,#176018,#176019,#176020,#176021,#176022,#176023,
#176024,#176025,#176026,#176027,#176028,#176029,#176030,#176031,#176032,
#176033,#176034,#176035,#176036,#176037,#176038,#176039,#176040,#176041,
#176042,#176043,#176044,#176045,#176046,#176047,#176048,#176049,#176050,
#176051,#176052,#176053,#176054,#176055,#176056,#176057,#176058,#176059,
#176060,#176061,#176062,#176063,#176064,#176065,#176066,#176067,#176068,
#176069,#176070,#176071,#176072,#176073,#176074,#176075,#176076,#176077,
#176078,#176079,#176080,#176081,#176082,#176083,#176084,#176085,#176086,
#176087,#176088,#176089,#176090,#176091,#176092,#176093,#176094,#176095,
#176096,#176097,#176098,#176099,#176100,#176101,#176102,#176103,#176104,
#176105,#176106,#176107,#176108,#176109,#176110,#176111,#176112,#176113,
#176114,#176115,#176116,#176117,#176118,#176119,#176120,#176121,#176122,
#176123,#176124,#176125,#176126,#176127,#176128,#176129,#176130,#176131,
#176132,#176133,#176134,#176135,#176136,#176137,#176138,#176139,#176140,
#176141,#176142,#176143,#176144,#176145,#176146,#176147,#176148,#176149,
#176150,#176151,#176152,#176153,#176154,#176155,#176156,#176157,#176158,
#176159,#176160,#176161,#176162,#176163,#176164,#176165,#176166,#176167,
#176168,#176169,#176170,#176171,#176172,#176173,#176174,#176175,#176176,
#176177,#176178,#176179,#176180,#176181,#176182,#176183,#176184,#176185,
#176186,#176187,#176188,#176189,#176190,#176191,#176192,#176193,#176194,
#176195,#176196,#176197,#176198,#176199,#176200,#176201,#176202,#176203,
#176204,#176205,#176206,#176207,#176208,#176209,#176210),.UNSPECIFIED.,
 .F.,.F.,(4,2,2,2,2,2,2,2,2,2,2,2,2,2,2,2,2,2,2,2,2,2,2,2,2,2,2,2,2,2,2,
2,2,2,2,2,2,2,2,2,2,2,2,2,2,2,2,2,2,2,2,2,2,2,2,2,2,2,2,2,2,2,2,2,2,2,2,
2,2,2,2,2,2,2,2,2,2,2,2,2,2,2,2,2,2,2,2,2,2,2,2,2,2,2,2,2,2,2,2,2,2,2,2,
2,2,2,2,2,2,2,2,2,2,4),(1.40869684638067,1.45282843584756,1.47139153129055,
1.47413797142721,1.47549374264355,1.47656594495266,1.47781700648748,1.48006379995523,
1.49092661598699,1.51513105515911,1.55576274020903,1.57471834154224,1.57847301714692,
1.58088008000737,1.58279806296705,1.58496219546508,1.58861933921804,1.60315458464438,
1.63040943645443,1.67885530689127,1.6848724182356,1.68679164489817,1.68797022456709,
1.68905892046346,1.69054582954117,1.69399109741873,1.72339037290005,1.74244927090556,
1.7857829634416,1.79007584733931,1.79261693152861,1.79455821379679,1.7966328302524,
1.7998849248117,1.81021815464008,1.82682882107904,1.85976403632507,1.87664269438957,
1.88258541443695,1.89582906497522,1.8980970124788,1.89947544063993,1.90055205795811,
1.9017728389302,1.90388172087427,1.91271551805827,1.93013747091191,1.98024680163006,
1.99885474444774,2.0025864252489,2.00498643324687,2.00690376651553,2.0090724765539,
2.01275030228118,2.02754321747452,2.0555561790587,2.10529260279538,2.10950546056186,
2.11116748441838,2.11217792702289,2.11328233968098,2.11485664842832,2.11882605818134,
2.13856756495848,2.16752538738815,2.20987543263793,2.2141699598811,2.21671152958959,
2.21865290204596,2.22072734256464,2.22397859237694,2.2343043333581,2.25089838425513,
2.28381993277496,2.299787081885,2.30320930710508,2.31967420772753,2.32231284691757,
2.32366452388258,2.32473648328883,2.3259907191237,2.32825190546424,2.33935483750962,
2.36446444931113,2.41873422061789,2.42552403892733,2.42837396756816,2.43016431875726,
2.43208993035218,2.43472297659844,2.4376774992918,2.44275935847805,2.4536356672814,
2.48468546992922,2.52883690999794,2.53346430380101,2.53519168928287,2.53621472676427,
2.5373092542562,2.53883045378196,2.54247536084109,2.55926024272092,2.61328639023885,
2.62540476019049,2.62723236323862,2.62823403157241,2.63692330652055,2.64007496601508,
2.64192232708146,2.64377759546468,2.6456459633452,2.64804781939747,2.65178836875005,
2.66842437218317),.UNSPECIFIED.);
#1841=B_SPLINE_CURVE_WITH_KNOTS('',3,(#176211,#176212,#176213,#176214,#176215,
#176216,#176217,#176218,#176219,#176220),.UNSPECIFIED.,.F.,.F.,(4,3,3,4),
(-85.8723819043546,-85.755698970363,-85.6390734987538,-85.5224480271446),
 .UNSPECIFIED.);
#1842=B_SPLINE_CURVE_WITH_KNOTS('',3,(#176225,#176226,#176227,#176228,#176229,
#176230,#176231,#176232,#176233,#176234,#176235,#176236,#176237,#176238,
#176239,#176240,#176241,#176242,#176243,#176244,#176245,#176246,#176247,
#176248,#176249,#176250,#176251,#176252,#176253,#176254,#176255,#176256,
#176257,#176258,#176259,#176260,#176261,#176262,#176263,#176264,#176265,
#176266,#176267,#176268,#176269,#176270,#176271,#176272,#176273,#176274,
#176275,#176276,#176277,#176278,#176279,#176280,#176281,#176282,#176283,
#176284,#176285,#176286,#176287,#176288,#176289,#176290,#176291,#176292,
#176293,#176294,#176295,#176296,#176297,#176298,#176299,#176300,#176301,
#176302,#176303,#176304,#176305,#176306,#176307,#176308,#176309,#176310,
#176311,#176312,#176313,#176314,#176315,#176316,#176317,#176318,#176319,
#176320,#176321,#176322,#176323,#176324,#176325,#176326,#176327,#176328,
#176329,#176330,#176331,#176332,#176333,#176334,#176335,#176336,#176337,
#176338,#176339,#176340,#176341,#176342,#176343,#176344,#176345,#176346,
#176347,#176348,#176349,#176350,#176351,#176352,#176353,#176354,#176355,
#176356,#176357,#176358,#176359,#176360,#176361,#176362,#176363,#176364,
#176365,#176366,#176367,#176368,#176369,#176370,#176371,#176372,#176373,
#176374,#176375,#176376,#176377,#176378,#176379,#176380,#176381,#176382,
#176383,#176384,#176385,#176386,#176387,#176388,#176389,#176390,#176391,
#176392,#176393,#176394,#176395,#176396,#176397,#176398,#176399,#176400,
#176401,#176402,#176403,#176404,#176405,#176406,#176407,#176408,#176409,
#176410,#176411,#176412,#176413,#176414,#176415,#176416,#176417,#176418,
#176419,#176420,#176421,#176422,#176423,#176424,#176425,#176426,#176427,
#176428,#176429,#176430,#176431,#176432,#176433,#176434,#176435,#176436,
#176437,#176438,#176439,#176440,#176441,#176442,#176443,#176444,#176445,
#176446,#176447,#176448,#176449,#176450,#176451,#176452,#176453,#176454,
#176455,#176456,#176457,#176458),.UNSPECIFIED.,.F.,.F.,(4,2,2,2,2,2,2,2,
2,2,2,2,2,2,2,2,2,2,2,2,2,2,2,2,2,2,2,2,2,2,2,2,2,2,2,2,2,2,2,2,2,2,2,2,
2,2,2,2,2,2,2,2,2,2,2,2,2,2,2,2,2,2,2,2,2,2,2,2,2,2,2,2,2,2,2,2,2,2,2,2,
2,2,2,2,2,2,2,2,2,2,2,2,2,2,2,2,2,2,2,2,2,2,2,2,2,2,2,2,2,2,2,2,2,2,2,2,
4),(1.25998791133046,1.26024242500464,1.26239919564322,1.26363040643267,
1.26470495450532,1.26608904347515,1.26897931713014,1.2946802036782,1.33412358883784,
1.36184468975562,1.365984948207,1.36848121557409,1.3704151048674,1.3725084082164,
1.37584668051751,1.38696194568658,1.40534596761406,1.45269478775345,1.47125602150215,
1.47400217378428,1.47535780193761,1.4764298906353,1.47768081907448,1.4799273721928,
1.49078900086812,1.51499074218715,1.5556182103993,1.57457185689772,1.57832613872912,
1.58073294772477,1.58265072748706,1.58481462973893,1.58847138205162,1.60300504053265,
1.63025686999265,1.67869647391258,1.68471398853011,1.68663314099338,1.68781162454298,
1.68890019358684,1.6903868751714,1.69383137905133,1.73244164718219,1.7820191168021,
1.78911702252191,1.79201778588942,1.79381727822345,1.79577415262608,1.79845378998335,
1.8047143767895,1.8319836912695,1.87335236275129,1.87999866272132,1.89550853911073,
1.89810753672073,1.89945057988605,1.90052186307516,1.90178248353017,1.90407348974339,
1.91570147049743,1.9428858704825,1.9941791754067,2.0011879871368,2.004073859346,
2.00587058789711,2.00782961014574,2.01052153930724,2.01685412987579,2.04471505668319,
2.09013785020724,2.1074391827338,2.11010913681588,2.11146742182158,2.11253974323807,
2.11378879751528,2.1160266407964,2.12674430957233,2.15041407152702,2.2068425921498,
2.21342049874239,2.2159526974858,2.21777704697382,2.21971728601298,2.22229824838344,
2.22800315716179,2.25094047087012,2.283951813764,2.30421150100962,2.30447940405299,
2.30917138770076,2.32002049487248,2.32215449014924,2.32350708441768,2.32457889711014,
2.32583195253543,2.32808847167246,2.33911822898416,2.3639527540638,2.41860981546139,
2.42536231845443,2.42820563734438,2.4299945240523,2.43192069962384,2.43455838914489,
2.43751954516248,2.44261831620993,2.45354607783007,2.48454341821539,2.52865262843015,
2.53326833133215,2.53499371288607,2.53601620908544,2.53711071152186,2.53863278588737,
2.54228406115615,2.55912777263654,2.59377040355344),.UNSPECIFIED.);
#1843=B_SPLINE_CURVE_WITH_KNOTS('',3,(#176460,#176461,#176462,#176463,#176464,
#176465,#176466,#176467,#176468,#176469,#176470,#176471,#176472,#176473,
#176474,#176475,#176476,#176477,#176478,#176479,#176480,#176481,#176482,
#176483,#176484,#176485,#176486,#176487,#176488,#176489,#176490,#176491,
#176492,#176493,#176494,#176495,#176496,#176497,#176498,#176499,#176500,
#176501,#176502,#176503,#176504,#176505,#176506,#176507,#176508,#176509,
#176510,#176511,#176512,#176513,#176514,#176515,#176516,#176517,#176518,
#176519,#176520,#176521,#176522,#176523,#176524,#176525,#176526,#176527,
#176528,#176529,#176530,#176531,#176532,#176533,#176534,#176535,#176536,
#176537,#176538,#176539,#176540,#176541,#176542,#176543,#176544,#176545,
#176546,#176547,#176548,#176549,#176550,#176551,#176552,#176553,#176554,
#176555,#176556,#176557,#176558,#176559,#176560,#176561,#176562,#176563,
#176564,#176565,#176566,#176567,#176568,#176569,#176570,#176571,#176572,
#176573,#176574,#176575,#176576,#176577,#176578,#176579,#176580,#176581,
#176582,#176583,#176584,#176585,#176586,#176587,#176588,#176589,#176590,
#176591,#176592,#176593,#176594,#176595,#176596,#176597,#176598,#176599,
#176600,#176601,#176602,#176603,#176604,#176605,#176606,#176607,#176608,
#176609,#176610,#176611,#176612,#176613,#176614,#176615,#176616,#176617,
#176618,#176619,#176620,#176621,#176622,#176623,#176624,#176625,#176626,
#176627,#176628,#176629,#176630,#176631,#176632,#176633,#176634,#176635,
#176636,#176637,#176638,#176639,#176640),.UNSPECIFIED.,.F.,.F.,(4,3,3,3,
3,3,3,3,3,3,3,3,3,3,3,3,3,3,3,3,3,3,3,3,3,3,3,3,3,3,3,3,3,3,3,3,3,3,3,3,
3,3,3,3,3,3,3,3,3,3,3,3,3,3,3,3,3,3,3,3,4),(-91.8056330559228,-91.7034783920473,
-91.6014794906875,-91.4995669524817,-91.3977052133723,-91.2958587787107,
-91.1939207704893,-91.0919397623294,-90.9897717066984,-90.8941169465306,
-90.7907222094827,-90.6874809273677,-90.5843609619754,-90.4813063937665,
-90.3782831854089,-90.2752573427364,-90.1721245759583,-90.0689354845485,
-89.9655634911669,-89.8952804965687,-89.7918857595208,-89.6886444774058,
-89.5855245120135,-89.4824699438045,-89.3794467354467,-89.2764208927743,
-89.1732881259961,-89.0700990345863,-88.9667270412046,-88.8964440466068,
-88.7930493095589,-88.6898080274442,-88.586688062052,-88.4836334938431,
-88.3806102854853,-88.2775844428131,-88.174451676035,-88.0712625846253,
-87.9678905912437,-87.897607596645,-87.7942128595971,-87.690971577482,-87.5878516120897,
-87.4847970438806,-87.3817738355228,-87.2787479928504,-87.1756152260724,
-87.0724261346626,-86.969054141281,-86.8987711466831,-86.7953764096351,
-86.6921351275202,-86.5890151621278,-86.4859605939189,-86.382937385561,
-86.2799115428888,-86.1767787761106,-86.0735896847007,-85.970217691319,
-85.8999346967212,-85.8723819043546),.UNSPECIFIED.);
#1844=B_SPLINE_CURVE_WITH_KNOTS('',3,(#176641,#176642,#176643,#176644,#176645),
 .UNSPECIFIED.,.F.,.F.,(4,1,4),(-92.1566391741352,-91.8929533964925,-91.8056333339369),
 .UNSPECIFIED.);
#1845=B_SPLINE_CURVE_WITH_KNOTS('',3,(#176651,#176652,#176653,#176654,#176655,
#176656,#176657,#176658,#176659,#176660,#176661,#176662,#176663,#176664,
#176665,#176666,#176667,#176668,#176669,#176670,#176671,#176672),
 .UNSPECIFIED.,.F.,.F.,(4,2,2,2,2,2,2,2,2,2,4),(2.59436936426754,2.62465525255589,
2.6484457796913,2.6563175990635,2.65841363975286,2.6596436413572,2.66070047280065,
2.66174639015292,2.66309684904183,2.66555495191749,2.6686486774568),
 .UNSPECIFIED.);
#1846=B_SPLINE_CURVE_WITH_KNOTS('',3,(#176673,#176674,#176675,#176676,#176677,
#176678,#176679,#176680,#176681,#176682,#176683,#176684,#176685,#176686,
#176687,#176688,#176689,#176690,#176691,#176692,#176693,#176694,#176695,
#176696,#176697,#176698,#176699,#176700,#176701,#176702,#176703,#176704,
#176705,#176706,#176707,#176708,#176709,#176710,#176711,#176712,#176713,
#176714,#176715,#176716,#176717,#176718,#176719,#176720,#176721,#176722,
#176723,#176724,#176725,#176726,#176727,#176728,#176729,#176730,#176731,
#176732,#176733,#176734,#176735,#176736,#176737,#176738,#176739,#176740,
#176741,#176742,#176743,#176744,#176745,#176746,#176747,#176748,#176749,
#176750,#176751,#176752,#176753,#176754,#176755,#176756,#176757,#176758,
#176759,#176760,#176761,#176762,#176763,#176764,#176765,#176766,#176767,
#176768,#176769,#176770,#176771,#176772,#176773,#176774,#176775,#176776,
#176777,#176778,#176779,#176780,#176781,#176782,#176783,#176784,#176785,
#176786,#176787,#176788,#176789,#176790,#176791,#176792,#176793,#176794,
#176795,#176796,#176797,#176798,#176799,#176800,#176801,#176802,#176803,
#176804,#176805,#176806,#176807,#176808,#176809,#176810,#176811,#176812,
#176813,#176814,#176815,#176816,#176817,#176818,#176819,#176820,#176821,
#176822,#176823,#176824,#176825,#176826,#176827,#176828,#176829,#176830,
#176831,#176832,#176833,#176834,#176835,#176836,#176837,#176838,#176839,
#176840,#176841,#176842,#176843,#176844,#176845,#176846,#176847,#176848,
#176849,#176850,#176851,#176852,#176853,#176854,#176855,#176856,#176857,
#176858,#176859,#176860,#176861,#176862,#176863,#176864,#176865,#176866,
#176867,#176868,#176869,#176870,#176871,#176872,#176873,#176874,#176875,
#176876,#176877,#176878,#176879,#176880,#176881,#176882,#176883,#176884,
#176885,#176886,#176887,#176888,#176889,#176890,#176891,#176892,#176893,
#176894,#176895,#176896,#176897,#176898,#176899,#176900),.UNSPECIFIED.,
 .F.,.F.,(4,2,2,2,2,2,2,2,2,2,2,2,2,2,2,2,2,2,2,2,2,2,2,2,2,2,2,2,2,2,2,
2,2,2,2,2,2,2,2,2,2,2,2,2,2,2,2,2,2,2,2,2,2,2,2,2,2,2,2,2,2,2,2,2,2,2,2,
2,2,2,2,2,2,2,2,2,2,2,2,2,2,2,2,2,2,2,2,2,2,2,2,2,2,2,2,2,2,2,2,2,2,2,2,
2,2,2,2,2,2,2,2,2,2,4),(0.000817344086041159,0.0612273919498641,0.0876740801193658,
0.0938319778978367,0.0964930492572893,0.098445916956004,0.10024843117888,
0.103169002752325,0.11039006372335,0.154190655546873,0.195390525340292,
0.199210997745504,0.201236633489129,0.202548493583,0.203772360348178,0.203775924959625,
0.20377950209078,0.20378309200526,0.203786919778984,0.20379080898577,0.203794761166127,
0.203798777733783,0.203802859832712,0.203807008834988,0.203811226399929,
0.20485382976206,0.206215941873864,0.208996272577505,0.228693719507084,
0.27474163152674,0.293140210772685,0.304261621807657,0.307599685704812,
0.309692404299447,0.311625444707257,0.314120185036224,0.31825700462144,
0.345888070718099,0.388200003981098,0.404174667384379,0.412512770760822,
0.414581741117975,0.415793247154152,0.416871061291057,0.418263154471234,
0.420578800539232,0.43480898130666,0.483112060256287,0.511251700506572,
0.517617119438996,0.520313936998886,0.52227319669367,0.524067850567381,
0.526945354508734,0.533908091086557,0.585900847573902,0.612587659650053,
0.624089895485527,0.626373200063177,0.627631823572945,0.628702764682022,
0.63004709293401,0.632653579135124,0.648359659618089,0.692810926181391,
0.715109505886791,0.727829795237389,0.731327778194906,0.733455972991943,
0.73537942610946,0.737844614280843,0.741792255381091,0.764379873525667,
0.823320016195228,0.835967143277367,0.838311346381681,0.839583216957975,
0.840653445551531,0.841981864392049,0.844037552281527,0.853719298631803,
0.859523384065908,0.859958365484185,0.866842920809183,0.880568808716069,
0.913426383209187,0.929986567229701,0.940296859256234,0.943545472397734,
0.945618772206083,0.947559458069651,0.950100679709231,0.954395885224703,
0.989519314416273,1.03844552960186,1.04822026746025,1.05039677999474,1.05163225416324,
1.05270602646014,1.05408323483342,1.05693879862438,1.07971753539956,1.09256085135529,
1.12541335058915,1.1419649645055,1.15227167883996,1.15552010055828,1.15759350313277,
1.15953444321355,1.16207622576685,1.16637289051967,1.20157678546922,1.25075405362961,
1.25998791133046),.UNSPECIFIED.);
#1847=B_SPLINE_CURVE_WITH_KNOTS('',3,(#176902,#176903,#176904,#176905,#176906,
#176907,#176908,#176909,#176910,#176911),.UNSPECIFIED.,.F.,.F.,(4,1,1,1,
1,1,1,4),(-98.0888186411165,-97.8859720962637,-96.8871356463018,-95.88829919634,
-94.8894627463781,-93.8906262964162,-92.8917898464543,-92.1566391741352),
 .UNSPECIFIED.);
#1848=B_SPLINE_CURVE_WITH_KNOTS('',3,(#176912,#176913,#176914,#176915,#176916,
#176917,#176918,#176919,#176920,#176921,#176922,#176923,#176924,#176925,
#176926,#176927,#176928,#176929,#176930,#176931),.UNSPECIFIED.,.F.,.F.,
(4,2,2,2,2,2,2,2,2,4),(0.000629226955841834,0.0468644005961875,0.0541763610534283,
0.0579973882184613,0.0612784598809704,0.0633586706615918,0.0652962163607798,
0.0678195720804087,0.0720540263829488,0.0751037223624835),.UNSPECIFIED.);
#1849=B_SPLINE_CURVE_WITH_KNOTS('',3,(#176936,#176937,#176938,#176939,#176940,
#176941,#176942,#176943,#176944,#176945,#176946,#176947,#176948,#176949,
#176950,#176951,#176952,#176953,#176954,#176955,#176956,#176957,#176958,
#176959,#176960,#176961,#176962,#176963,#176964,#176965,#176966,#176967,
#176968,#176969,#176970,#176971,#176972,#176973,#176974,#176975,#176976,
#176977,#176978,#176979,#176980,#176981,#176982,#176983,#176984,#176985,
#176986,#176987,#176988,#176989,#176990,#176991,#176992,#176993,#176994,
#176995,#176996,#176997,#176998,#176999,#177000,#177001,#177002,#177003,
#177004,#177005,#177006,#177007,#177008,#177009,#177010,#177011,#177012,
#177013,#177014,#177015,#177016,#177017,#177018,#177019,#177020,#177021,
#177022,#177023,#177024,#177025,#177026,#177027,#177028,#177029,#177030,
#177031,#177032,#177033,#177034,#177035,#177036,#177037,#177038,#177039,
#177040,#177041,#177042,#177043,#177044,#177045,#177046,#177047,#177048,
#177049,#177050,#177051,#177052,#177053,#177054,#177055,#177056,#177057,
#177058,#177059,#177060,#177061,#177062,#177063,#177064,#177065,#177066,
#177067,#177068,#177069,#177070,#177071,#177072,#177073,#177074,#177075,
#177076,#177077,#177078,#177079,#177080,#177081,#177082,#177083,#177084,
#177085,#177086,#177087,#177088,#177089,#177090,#177091,#177092,#177093,
#177094,#177095,#177096,#177097,#177098,#177099,#177100,#177101,#177102,
#177103,#177104,#177105,#177106,#177107,#177108,#177109,#177110,#177111,
#177112,#177113,#177114,#177115,#177116,#177117,#177118,#177119,#177120,
#177121,#177122,#177123,#177124,#177125,#177126,#177127,#177128,#177129,
#177130,#177131,#177132,#177133,#177134,#177135,#177136,#177137,#177138,
#177139,#177140,#177141,#177142,#177143,#177144,#177145,#177146,#177147,
#177148,#177149,#177150,#177151,#177152,#177153,#177154,#177155,#177156,
#177157,#177158,#177159,#177160,#177161,#177162,#177163,#177164,#177165,
#177166,#177167,#177168,#177169,#177170,#177171,#177172,#177173),
 .UNSPECIFIED.,.F.,.F.,(4,2,2,2,2,2,2,2,2,2,2,2,2,2,2,2,2,2,2,2,2,2,2,2,
2,2,2,2,2,2,2,2,2,2,2,2,2,2,2,2,2,2,2,2,2,2,2,2,2,2,2,2,2,2,2,2,2,2,2,2,
2,2,2,2,2,2,2,2,2,2,2,2,2,2,2,2,2,2,2,2,2,2,2,2,2,2,2,2,2,2,2,2,2,2,2,2,
2,2,2,2,2,2,2,2,2,2,2,2,2,2,2,2,2,2,2,2,2,2,4),(1.2602735482109,1.26524054933663,
1.27572678542071,1.27899648729593,1.2810750955584,1.28301505575824,1.28554714969485,
1.28980869553093,1.33481507250788,1.37987265493806,1.38459854900304,1.38634110502145,
1.38736724901935,1.38846010627813,1.3899708367368,1.39355297507645,1.43119610811479,
1.48162620370429,1.48868576676276,1.49158060582017,1.49337936338234,1.49533777291039,
1.49802373704153,1.50431857130575,1.53186137828442,1.56026918777434,1.5826023287173,
1.59531105022385,1.5975519259267,1.59893716540897,1.60001213077348,1.60124329461293,
1.60339872973208,1.61286169964153,1.66205401313269,1.69726375900075,1.70156163028444,
1.70410423789648,1.70604586115812,1.70812004416496,1.7113697930735,1.72168151420924,
1.73824423161456,1.77114074799051,1.78487809342853,1.79175063948774,1.79196058592751,
1.79531500384449,1.80743272705653,1.80964180457274,1.81101740113463,1.81209135996309,
1.81332868926533,1.81551239220539,1.82538521736245,1.87422390424592,1.90932066511989,
1.91361678748023,1.91615879605051,1.91810021275967,1.92017441839195,1.92342471074427,
1.93374243897526,1.95031888046098,1.9832254465123,1.9980832698433,2.00311584368939,
2.01914780776842,2.02176933599478,2.02311731833539,2.02418900962129,2.02544601531626,
2.02772000984015,2.03904389303407,2.06501019048752,2.11803206612321,2.12492422933445,
2.12779102136437,2.1295843971836,2.13154660584663,2.13425542872474,2.14068665178564,
2.16936621182781,2.22067137106803,2.2316908521092,2.23383583469551,2.23519193710948,
2.23626421898748,2.23751516357257,2.23976122283613,2.25061039974527,2.27476320132649,
2.33046247571524,2.33711872183493,2.33966348919224,2.34149130584987,2.34343008919646,
2.34600035908364,2.35164587457701,2.37414026249403,2.40687040215125,2.44298543729769,
2.44584303621401,2.44722085728533,2.44826025588754,2.44945571223507,2.45072982857325,
2.45266376421573,2.45624155504831,2.46471622201167,2.52444415254189,2.54624111812614,
2.55015681175158,2.55261285073262,2.55453587262887,2.55667046904025,2.56019486561849,
2.57319060392375,2.59436936426754),.UNSPECIFIED.);
#1850=B_SPLINE_CURVE_WITH_KNOTS('',3,(#177174,#177175,#177176,#177177,#177178,
#177179,#177180,#177181,#177182,#177183,#177184,#177185,#177186,#177187,
#177188,#177189,#177190,#177191,#177192,#177193,#177194,#177195,#177196,
#177197,#177198,#177199,#177200,#177201,#177202,#177203,#177204,#177205,
#177206,#177207,#177208,#177209,#177210,#177211,#177212,#177213,#177214,
#177215,#177216,#177217,#177218,#177219,#177220,#177221,#177222,#177223,
#177224,#177225,#177226,#177227,#177228,#177229,#177230,#177231,#177232,
#177233,#177234,#177235,#177236,#177237,#177238,#177239,#177240,#177241,
#177242,#177243,#177244,#177245,#177246,#177247,#177248,#177249,#177250,
#177251,#177252,#177253,#177254,#177255,#177256,#177257,#177258,#177259,
#177260,#177261,#177262,#177263,#177264,#177265,#177266,#177267,#177268,
#177269,#177270,#177271,#177272,#177273,#177274,#177275,#177276,#177277,
#177278,#177279,#177280,#177281,#177282,#177283,#177284,#177285,#177286,
#177287,#177288,#177289,#177290,#177291,#177292,#177293,#177294,#177295,
#177296,#177297,#177298,#177299,#177300,#177301,#177302,#177303,#177304,
#177305,#177306,#177307,#177308,#177309,#177310,#177311,#177312,#177313,
#177314,#177315,#177316,#177317,#177318,#177319,#177320,#177321,#177322,
#177323,#177324,#177325,#177326,#177327,#177328,#177329,#177330,#177331,
#177332,#177333,#177334,#177335,#177336,#177337,#177338,#177339,#177340,
#177341,#177342,#177343,#177344,#177345,#177346,#177347,#177348,#177349,
#177350,#177351,#177352,#177353,#177354,#177355,#177356,#177357,#177358,
#177359,#177360,#177361,#177362,#177363,#177364,#177365,#177366,#177367,
#177368,#177369,#177370,#177371,#177372,#177373,#177374,#177375,#177376,
#177377,#177378,#177379,#177380,#177381,#177382,#177383,#177384,#177385,
#177386,#177387,#177388,#177389,#177390,#177391,#177392,#177393,#177394,
#177395,#177396,#177397,#177398,#177399),.UNSPECIFIED.,.F.,.F.,(4,2,2,2,
2,2,2,2,2,2,2,2,2,2,2,2,2,2,2,2,2,2,2,2,2,2,2,2,2,2,2,2,2,2,2,2,2,2,2,2,
2,2,2,2,2,2,2,2,2,2,2,2,2,2,2,2,2,2,2,2,2,2,2,2,2,2,2,2,2,2,2,2,2,2,2,2,
2,2,2,2,2,2,2,2,2,2,2,2,2,2,2,2,2,2,2,2,2,2,2,2,2,2,2,2,2,2,2,2,2,2,2,2,
4),(0.0751037223624835,0.118900071491345,0.139440611476386,0.162494609014913,
0.166929447372164,0.168203542012268,0.16941891659701,0.170495934977998,
0.171881528995767,0.17417499241479,0.187957175240597,0.190682887305246,
0.190933904540755,0.199768469865087,0.24375060366284,0.259912600165475,
0.270000149625801,0.273247427352306,0.27532023318146,0.27726070839858,0.279802017491679,
0.284098185254886,0.319339705674213,0.368614641292319,0.377961258390835,
0.380107549102336,0.381336258131637,0.382410885506348,0.383798058387966,
0.386046712681178,0.398924057679309,0.401653712218978,0.405940989869747,
0.448932565391636,0.476872490705792,0.483214204736425,0.485907202932065,
0.487865973176792,0.489661760994714,0.492544552608456,0.499537871890721,
0.551075277271631,0.578095800714917,0.589681412156881,0.59196960561499,
0.593229390121345,0.594300394767089,0.595643630561402,0.598244579921869,
0.613814860738228,0.620269138462949,0.661687588346286,0.688961708677915,
0.695222503312131,0.697901721679331,0.699858103700696,0.701657017221726,
0.704556556685558,0.711650019409065,0.761312279955728,0.799626380882392,
0.803230961460248,0.804745028476189,0.805838017498936,0.806862472882087,
0.808598302539427,0.813283520889909,0.854368024800134,0.900801490929616,
0.907193854351943,0.909895570960788,0.911856010895325,0.913650103924896,
0.916523120549423,0.923456525761156,0.975907063984641,1.00228278043963,
1.01370811533073,1.01598740384887,1.0172453106221,1.01831654721534,1.01966239680701,
1.02227520012398,1.0381277176306,1.0428721627749,1.0581510675028,1.09102885175531,
1.10761165021532,1.1179323842797,1.1211823533058,1.12325605403864,1.12519678906149,
1.12773760466332,1.13203106984393,1.17443434157364,1.20349382106149,1.22311111557103,
1.22706657205871,1.22863835153548,1.22974200779255,1.2307525433553,1.23241627501659,
1.2366416743528,1.28598846466241,1.32675994086166,1.33182657063566,1.33428638208849,
1.33620950461565,1.33834128821519,1.34185428160786,1.3547312148031,1.37743522651096,
1.40858865855495),.UNSPECIFIED.);
#1851=B_SPLINE_CURVE_WITH_KNOTS('',3,(#177405,#177406,#177407,#177408),
 .UNSPECIFIED.,.F.,.F.,(4,4),(114.406674973147,114.756144634991),
 .UNSPECIFIED.);
#1852=B_SPLINE_CURVE_WITH_KNOTS('',3,(#177409,#177410,#177411,#177412,#177413,
#177414,#177415,#177416,#177417,#177418,#177419,#177420,#177421,#177422,
#177423,#177424,#177425,#177426,#177427,#177428,#177429,#177430,#177431,
#177432,#177433,#177434,#177435,#177436,#177437,#177438,#177439,#177440,
#177441,#177442,#177443,#177444,#177445,#177446,#177447,#177448,#177449,
#177450,#177451,#177452,#177453,#177454,#177455,#177456,#177457,#177458,
#177459,#177460,#177461,#177462,#177463,#177464,#177465,#177466,#177467,
#177468,#177469,#177470,#177471,#177472,#177473,#177474,#177475,#177476,
#177477,#177478,#177479,#177480,#177481,#177482,#177483,#177484,#177485,
#177486,#177487,#177488,#177489,#177490,#177491,#177492,#177493,#177494,
#177495,#177496,#177497,#177498,#177499,#177500,#177501,#177502,#177503,
#177504,#177505,#177506,#177507,#177508,#177509,#177510,#177511,#177512,
#177513,#177514,#177515,#177516,#177517,#177518,#177519,#177520,#177521,
#177522,#177523,#177524,#177525,#177526,#177527,#177528,#177529,#177530,
#177531,#177532,#177533,#177534,#177535,#177536,#177537,#177538,#177539,
#177540,#177541,#177542,#177543,#177544,#177545,#177546,#177547,#177548,
#177549,#177550,#177551,#177552,#177553,#177554,#177555,#177556,#177557,
#177558,#177559,#177560,#177561,#177562,#177563,#177564,#177565,#177566,
#177567,#177568,#177569,#177570,#177571,#177572,#177573,#177574,#177575,
#177576,#177577,#177578,#177579,#177580,#177581,#177582,#177583,#177584,
#177585,#177586,#177587,#177588,#177589,#177590,#177591,#177592,#177593,
#177594,#177595,#177596,#177597,#177598,#177599,#177600,#177601,#177602,
#177603,#177604,#177605,#177606,#177607,#177608,#177609,#177610,#177611,
#177612,#177613,#177614,#177615,#177616,#177617,#177618,#177619,#177620,
#177621,#177622,#177623,#177624),.UNSPECIFIED.,.F.,.F.,(4,2,2,2,2,2,2,2,
2,2,2,2,2,2,2,2,2,2,2,2,2,2,2,2,2,2,2,2,2,2,2,2,2,2,2,2,2,2,2,2,2,2,2,2,
2,2,2,2,2,2,2,2,2,2,2,2,2,2,2,2,2,2,2,2,2,2,2,2,2,2,2,2,2,2,2,2,2,2,2,2,
2,2,2,2,2,2,2,2,2,2,2,2,2,2,2,2,2,2,2,2,2,2,2,2,2,2,2,4),(0.000658788743625867,
0.00332970120247789,0.0059216581112381,0.00778879636083556,0.00964368915836675,
0.0114909184573996,0.0146445377481801,0.0233614972363175,0.0916990880801217,
0.109068193657669,0.112778808087098,0.114310760389999,0.11540697933727,
0.116426840351137,0.118138930635243,0.122667883778095,0.169431857768071,
0.208758990986267,0.213873118206603,0.216840473135931,0.218921510588389,
0.220936589487488,0.222824536013458,0.225367120679629,0.229666778264646,
0.264877030777271,0.314097831342373,0.323532822729939,0.325685733763093,
0.326916056242964,0.327990681575802,0.329375991757707,0.332272740972979,
0.358675098332123,0.367914145845947,0.400741271683807,0.417260994262733,
0.427553432816872,0.430800331440078,0.432873478033103,0.434814681886291,
0.437357536618714,0.441657643812989,0.476789978187575,0.525756231602942,
0.535494695252995,0.537668971011242,0.538904077655923,0.539978108504761,
0.541356404323984,0.544216825744425,0.580267587356483,0.612981104505948,
0.635495272040016,0.641143633966508,0.643714316398006,0.645653053004703,
0.647480566482349,0.650024495973927,0.656676003782097,0.71244616816722,
0.736576055135473,0.747418055806598,0.749663601083023,0.750914381459764,
0.751986601753206,0.75334272058979,0.756002307100268,0.773020197169769,
0.823201341733096,0.840782435432029,0.851549275611795,0.854849905626905,
0.856935048636541,0.858872028085661,0.861387314033059,0.865592071978735,
0.895849861764218,0.947380641155931,0.959374744285399,0.961685910910082,
0.962950974924926,0.964022068207264,0.965359863396906,0.967445076168874,
0.977540170700345,0.983029053873848,0.9924188375024,1.00399162343487,1.03684321083926,
1.0533867454283,1.06369065632845,1.06693938111617,1.06901326248663,1.07095485129084,
1.07349777279795,1.07779701178068,1.11311224973216,1.1623737843867,1.17171279034325,
1.17385935466317,1.17508854481749,1.17616380431521,1.17755207184592,1.18046252839983,
1.20859761461961,1.24829263426394,1.2602735482109),.UNSPECIFIED.);
#1853=B_SPLINE_CURVE_WITH_KNOTS('',3,(#177626,#177627,#177628,#177629,#177630,
#177631,#177632,#177633,#177634,#177635,#177636,#177637,#177638,#177639,
#177640,#177641,#177642,#177643,#177644,#177645,#177646,#177647,#177648,
#177649,#177650,#177651,#177652,#177653,#177654,#177655,#177656,#177657,
#177658,#177659,#177660,#177661,#177662,#177663,#177664,#177665,#177666,
#177667,#177668,#177669,#177670,#177671,#177672,#177673,#177674,#177675,
#177676,#177677,#177678,#177679,#177680,#177681,#177682,#177683,#177684,
#177685,#177686,#177687,#177688,#177689,#177690,#177691,#177692,#177693,
#177694,#177695,#177696,#177697,#177698,#177699,#177700,#177701,#177702,
#177703,#177704,#177705,#177706,#177707,#177708,#177709,#177710,#177711,
#177712,#177713,#177714,#177715,#177716,#177717,#177718,#177719,#177720,
#177721,#177722,#177723,#177724,#177725,#177726,#177727,#177728,#177729,
#177730,#177731,#177732,#177733,#177734,#177735,#177736,#177737,#177738,
#177739,#177740,#177741,#177742,#177743,#177744,#177745,#177746,#177747,
#177748,#177749,#177750,#177751,#177752,#177753,#177754,#177755,#177756,
#177757,#177758,#177759,#177760,#177761,#177762,#177763,#177764,#177765,
#177766,#177767,#177768,#177769,#177770,#177771,#177772,#177773,#177774,
#177775,#177776,#177777,#177778,#177779,#177780,#177781,#177782,#177783,
#177784,#177785,#177786,#177787,#177788,#177789,#177790,#177791,#177792,
#177793,#177794,#177795,#177796,#177797,#177798,#177799,#177800,#177801,
#177802,#177803,#177804,#177805,#177806,#177807,#177808,#177809,#177810,
#177811,#177812,#177813,#177814,#177815,#177816,#177817,#177818,#177819,
#177820,#177821,#177822,#177823,#177824,#177825,#177826,#177827,#177828,
#177829,#177830,#177831,#177832,#177833,#177834,#177835,#177836,#177837,
#177838,#177839,#177840,#177841,#177842,#177843,#177844,#177845,#177846,
#177847),.UNSPECIFIED.,.F.,.F.,(4,2,2,2,2,2,2,2,2,2,2,2,2,2,2,2,2,2,2,2,
2,2,2,2,2,2,2,2,2,2,2,2,2,2,2,2,2,2,2,2,2,2,2,2,2,2,2,2,2,2,2,2,2,2,2,2,
2,2,2,2,2,2,2,2,2,2,2,2,2,2,2,2,2,2,2,2,2,2,2,2,2,2,2,2,2,2,2,2,2,2,2,2,
2,2,2,2,2,2,2,2,2,2,2,2,2,2,2,2,2,2,4),(1.40858865855495,1.41602849107768,
1.4210231606735,1.43703140374578,1.43965097151703,1.44099826580354,1.44206957836628,
1.44332633491721,1.44560037454426,1.45693465181834,1.48294808340535,1.5358716731755,
1.54276761216823,1.54563443688785,1.5474273867354,1.54938877055155,1.55209579696157,
1.55851964063635,1.58714587007974,1.63843210451319,1.64949485401555,1.65164202046835,
1.65299855082524,1.65407053545689,1.65532040249688,1.65756270368058,1.66835879189345,
1.69232031536541,1.74827928178904,1.75490511378606,1.7574446028402,1.75927063232313,
1.76120936507317,1.76378270830783,1.7694477780549,1.79209323471846,1.82491410613751,
1.82944508984973,1.86063062017755,1.86354284731735,1.86493104121718,1.86600581705397,
1.86723398626325,1.86937765641769,1.87868716725339,1.92782912581056,1.96320834519401,
1.96750626277942,1.97004819672523,1.97198890199243,1.97406171321363,1.97730849662109,
1.98760393538259,2.00413396908774,2.03699317678459,2.04850576240806,2.05831797706443,
2.05928071067701,2.07315419502193,2.07545386849614,2.07684132368472,2.07791861932185,
2.07913300412101,2.08121463403849,2.08970840087768,2.10612935253362,2.14859391205347,
2.17544941434954,2.17956641545037,2.18205546974822,2.1839878181852,2.18608350100494,
2.18943435217851,2.20067379356902,2.21934915538903,2.25535871683837,2.2845047971253,
2.28741809983126,2.28880643182995,2.28988114218869,2.29110904377492,2.29325179528874,
2.30255034156427,2.32140687507338,2.36918815777812,2.38807314822581,2.39182142641946,
2.39422593662769,2.39614288395535,2.39830691098425,2.40196645835302,2.41632806420291,
2.46677742008986,2.49647220492018,2.4993863770695,2.50077489989936,2.50184965515534,
2.50307749306043,2.50436930487639,2.50901370182217,2.53314924658976,2.55405337848608,
2.59909887046265,2.60335602728437,2.60588609608324,2.60782483170709,2.60990244605974,
2.61317125300074,2.6169746226263,2.62423948308767,2.6678681477495),
 .UNSPECIFIED.);
#1854=B_SPLINE_CURVE_WITH_KNOTS('',3,(#177848,#177849,#177850,#177851,#177852,
#177853,#177854,#177855,#177856,#177857,#177858,#177859,#177860,#177861,
#177862,#177863,#177864,#177865,#177866,#177867),.UNSPECIFIED.,.F.,.F.,
(4,2,2,2,2,2,2,2,2,4),(0.000649987072770544,0.0375152697013956,0.0412926013848847,
0.0433020282469795,0.0446072095719178,0.0458444128962429,0.0469177253289979,
0.0482917844166712,0.0511320530737365,0.0747588723678276),.UNSPECIFIED.);
#1855=B_SPLINE_CURVE_WITH_KNOTS('',3,(#177873,#177874,#177875,#177876,#177877,
#177878,#177879,#177880,#177881,#177882),.UNSPECIFIED.,.F.,.F.,(4,3,3,4),
(120.689857252469,120.859210445387,120.962579625196,121.040543944395),
 .UNSPECIFIED.);
#1856=B_SPLINE_CURVE_WITH_KNOTS('',3,(#177883,#177884,#177885,#177886,#177887,
#177888,#177889,#177890,#177891,#177892),.UNSPECIFIED.,.F.,.F.,(4,1,1,1,
1,1,1,4),(114.756144634991,114.866191745616,115.865028195577,116.863864645539,
117.862701095501,118.861537545463,119.860373995425,120.689851222995),
 .UNSPECIFIED.);
#1857=B_SPLINE_CURVE_WITH_KNOTS('',3,(#177893,#177894,#177895,#177896,#177897,
#177898,#177899,#177900,#177901,#177902,#177903,#177904,#177905,#177906,
#177907,#177908,#177909,#177910,#177911,#177912,#177913,#177914,#177915,
#177916,#177917,#177918,#177919,#177920,#177921,#177922,#177923,#177924,
#177925,#177926,#177927,#177928,#177929,#177930,#177931,#177932,#177933,
#177934,#177935,#177936,#177937,#177938,#177939,#177940,#177941,#177942,
#177943,#177944,#177945,#177946,#177947,#177948,#177949,#177950,#177951,
#177952,#177953,#177954,#177955,#177956,#177957,#177958,#177959,#177960,
#177961,#177962,#177963,#177964,#177965,#177966,#177967,#177968,#177969,
#177970,#177971,#177972,#177973,#177974,#177975,#177976,#177977,#177978,
#177979,#177980,#177981,#177982,#177983,#177984,#177985,#177986,#177987,
#177988,#177989,#177990,#177991,#177992,#177993,#177994,#177995,#177996,
#177997,#177998,#177999,#178000,#178001,#178002,#178003,#178004,#178005,
#178006,#178007,#178008,#178009,#178010,#178011,#178012,#178013,#178014,
#178015,#178016,#178017,#178018,#178019,#178020,#178021,#178022,#178023,
#178024,#178025,#178026,#178027,#178028,#178029,#178030,#178031,#178032,
#178033,#178034,#178035,#178036,#178037,#178038,#178039,#178040,#178041,
#178042,#178043,#178044,#178045,#178046,#178047,#178048,#178049,#178050,
#178051,#178052,#178053,#178054,#178055,#178056,#178057,#178058,#178059,
#178060,#178061,#178062,#178063,#178064,#178065,#178066,#178067,#178068,
#178069,#178070,#178071,#178072,#178073,#178074,#178075,#178076,#178077,
#178078,#178079,#178080,#178081,#178082,#178083,#178084,#178085,#178086,
#178087,#178088,#178089,#178090,#178091,#178092,#178093,#178094,#178095,
#178096,#178097,#178098,#178099,#178100,#178101,#178102,#178103,#178104,
#178105,#178106,#178107,#178108,#178109,#178110),.UNSPECIFIED.,.F.,.F.,
(4,2,2,2,2,2,2,2,2,2,2,2,2,2,2,2,2,2,2,2,2,2,2,2,2,2,2,2,2,2,2,2,2,2,2,
2,2,2,2,2,2,2,2,2,2,2,2,2,2,2,2,2,2,2,2,2,2,2,2,2,2,2,2,2,2,2,2,2,2,2,2,
2,2,2,2,2,2,2,2,2,2,2,2,2,2,2,2,2,2,2,2,2,2,2,2,2,2,2,2,2,2,2,2,2,2,2,2,
2,4),(0.0747588723678276,0.0879796870983175,0.109399101208918,0.13618200070148,
0.146436008192385,0.149706910345542,0.151785007961068,0.153723603728772,
0.156252645034177,0.160506226082512,0.193184719377548,0.222553895549607,
0.244173746486992,0.254295207460528,0.256485209434715,0.257733363566383,
0.258805364662574,0.260163818127456,0.262835836630906,0.28021576098978,
0.329253098414348,0.347302093622868,0.354571911865477,0.360001937435935,
0.36256736563645,0.364504735539526,0.366332872841691,0.368880746680496,
0.375561147398386,0.430980131140095,0.455321514737903,0.466218694672533,
0.468466988707819,0.469718090656642,0.47078984233517,0.472144414782186,
0.474886382538451,0.493336671015449,0.53746151312653,0.565332015013005,
0.571665398652692,0.574357014768523,0.576315572444477,0.578111714706853,
0.580996281507104,0.58800006481441,0.639382577525078,0.666515101842847,
0.678128410237519,0.680418185136889,0.681678330270937,0.68274933451004,
0.684092180670403,0.686691242532328,0.702216224453772,0.708761609068164,
0.722633933763404,0.755493995474727,0.772056493671663,0.782367915966502,
0.785616719921701,0.787690101784928,0.789630836549942,0.792172081959859,
0.79646723740172,0.831578360720192,0.880465480908942,0.89028867255224,0.892468531051077,
0.893704762858457,0.894778464033976,0.896154628445178,0.899004756030601,
0.93537470931285,0.989163092423328,0.995619144932156,0.998331712584215,
1.00029420667142,1.00208618009099,1.00494710651599,1.01180638634181,1.0652449889484,
1.09093524626958,1.10218664638406,1.10445606410749,1.10571187269424,1.10678335725249,
1.10813211021972,1.1107581751194,1.12692235755853,1.17758035248144,1.20199434245457,
1.20789436377431,1.21051042826656,1.21245612656223,1.21427052293804,1.21676513158997,
1.22311497510759,1.28150396882532,1.30395462441549,1.31433184317185,1.31654824759285,
1.31779253336388,1.31886525744178,1.32022985175578,1.32240326195016,1.33389996509002,
1.38263557238681,1.40832430342818),.UNSPECIFIED.);
#1858=B_SPLINE_CURVE_WITH_KNOTS('',3,(#178116,#178117,#178118,#178119,#178120,
#178121,#178122,#178123),.UNSPECIFIED.,.F.,.F.,(4,2,2,4),(2.59362475265785,
2.59837330782392,2.62640672493038,2.66809195083791),.UNSPECIFIED.);
#1859=B_SPLINE_CURVE_WITH_KNOTS('',3,(#178124,#178125,#178126,#178127,#178128,
#178129,#178130,#178131,#178132,#178133,#178134,#178135,#178136,#178137,
#178138,#178139,#178140,#178141,#178142,#178143,#178144,#178145,#178146,
#178147,#178148,#178149,#178150,#178151,#178152,#178153,#178154,#178155,
#178156,#178157,#178158,#178159,#178160,#178161,#178162,#178163,#178164,
#178165,#178166,#178167,#178168,#178169,#178170,#178171,#178172,#178173,
#178174,#178175,#178176,#178177,#178178,#178179,#178180,#178181,#178182,
#178183,#178184,#178185,#178186,#178187,#178188,#178189,#178190,#178191,
#178192,#178193,#178194,#178195,#178196,#178197,#178198,#178199,#178200,
#178201,#178202,#178203,#178204,#178205,#178206,#178207,#178208,#178209,
#178210,#178211,#178212,#178213,#178214,#178215,#178216,#178217,#178218,
#178219,#178220,#178221,#178222,#178223,#178224,#178225,#178226,#178227,
#178228,#178229,#178230,#178231,#178232,#178233,#178234,#178235,#178236,
#178237,#178238,#178239,#178240,#178241,#178242,#178243,#178244,#178245,
#178246,#178247,#178248,#178249,#178250,#178251,#178252,#178253,#178254,
#178255,#178256,#178257,#178258,#178259,#178260,#178261,#178262,#178263,
#178264,#178265,#178266,#178267,#178268,#178269,#178270,#178271,#178272,
#178273,#178274,#178275,#178276,#178277,#178278,#178279,#178280,#178281,
#178282,#178283,#178284,#178285,#178286,#178287,#178288,#178289,#178290,
#178291,#178292,#178293,#178294,#178295,#178296,#178297,#178298,#178299,
#178300,#178301),.UNSPECIFIED.,.F.,.F.,(4,3,3,3,3,3,3,3,3,3,3,3,3,3,3,3,
3,3,3,3,3,3,3,3,3,3,3,3,3,3,3,3,3,3,3,3,3,3,3,3,3,3,3,3,3,3,3,3,3,3,3,3,
3,3,3,3,3,3,3,4),(121.040543944395,121.143685152638,121.246752606079,121.349780357811,
121.452802409466,121.555926033343,121.659098496058,121.762462007832,121.858046895349,
121.961441632397,122.064682914512,122.167802879905,122.270857448114,122.373880656472,
122.476906499145,122.580039265923,122.683228357333,122.786600350715,122.856883345311,
122.960278082359,123.063519364473,123.166639329865,123.269693898074,123.372717106431,
123.475742949104,123.578875715882,123.682064807291,123.785436800672,123.855719795272,
123.95911453232,124.062355814435,124.165475779827,124.268530348036,124.371553556393,
124.474579399066,124.577712165844,124.680901257254,124.784273250635,124.854556245234,
124.957950982282,125.061192264397,125.16431222979,125.267366797999,125.370390006357,
125.47341584903,125.576548615808,125.679737707218,125.7831097006,125.853392695196,
125.956787432244,126.060028714359,126.163148679751,126.26620324796,126.369226456318,
126.472252298991,126.575385065769,126.678574157178,126.78194615056,126.852229145158,
126.973042559648),.UNSPECIFIED.);
#1860=B_SPLINE_CURVE_WITH_KNOTS('',3,(#178303,#178304,#178305,#178306,#178307,
#178308,#178309,#178310,#178311,#178312,#178313,#178314,#178315,#178316,
#178317,#178318,#178319,#178320,#178321,#178322,#178323,#178324,#178325,
#178326,#178327,#178328,#178329,#178330,#178331,#178332,#178333,#178334,
#178335,#178336,#178337,#178338,#178339,#178340,#178341,#178342,#178343,
#178344,#178345,#178346,#178347,#178348,#178349,#178350,#178351,#178352,
#178353,#178354,#178355,#178356,#178357,#178358,#178359,#178360,#178361,
#178362,#178363,#178364,#178365,#178366,#178367,#178368,#178369,#178370,
#178371,#178372,#178373,#178374,#178375,#178376,#178377,#178378,#178379,
#178380,#178381,#178382,#178383,#178384,#178385,#178386,#178387,#178388,
#178389,#178390,#178391,#178392,#178393,#178394,#178395,#178396,#178397,
#178398,#178399,#178400,#178401,#178402,#178403,#178404,#178405,#178406,
#178407,#178408,#178409,#178410,#178411,#178412,#178413,#178414,#178415,
#178416,#178417,#178418,#178419,#178420,#178421,#178422,#178423,#178424,
#178425,#178426,#178427,#178428,#178429,#178430,#178431,#178432,#178433,
#178434,#178435,#178436,#178437,#178438,#178439,#178440,#178441,#178442,
#178443,#178444,#178445,#178446,#178447,#178448,#178449,#178450,#178451,
#178452,#178453,#178454,#178455,#178456,#178457,#178458,#178459,#178460,
#178461,#178462,#178463,#178464,#178465,#178466,#178467,#178468,#178469,
#178470,#178471,#178472,#178473,#178474,#178475,#178476,#178477,#178478,
#178479,#178480,#178481,#178482,#178483,#178484,#178485,#178486,#178487,
#178488,#178489,#178490,#178491,#178492,#178493,#178494,#178495,#178496,
#178497,#178498,#178499,#178500,#178501,#178502,#178503,#178504,#178505,
#178506,#178507,#178508,#178509,#178510,#178511,#178512,#178513,#178514,
#178515,#178516,#178517,#178518,#178519,#178520),.UNSPECIFIED.,.F.,.F.,
(4,2,2,2,2,2,2,2,2,2,2,2,2,2,2,2,2,2,2,2,2,2,2,2,2,2,2,2,2,2,2,2,2,2,2,
2,2,2,2,2,2,2,2,2,2,2,2,2,2,2,2,2,2,2,2,2,2,2,2,2,2,2,2,2,2,2,2,2,2,2,2,
2,2,2,2,2,2,2,2,2,2,2,2,2,2,2,2,2,2,2,2,2,2,2,2,2,2,2,2,2,2,2,2,2,2,2,2,
2,4),(1.40832430342818,1.41583884775361,1.42010270180147,1.42263499298702,
1.42457441334773,1.42665176850529,1.42991807905246,1.4403811399291,1.45728209141941,
1.49511037311192,1.5251859935497,1.52810058477316,1.52948936141789,1.53056433804064,
1.5317924566932,1.53393538295632,1.54323153886664,1.56207808036235,1.60247855626088,
1.61474065051465,1.62934649672079,1.633134775163,1.6353497648843,1.63726202411854,
1.63959705367887,1.6440469755749,1.67495966545922,1.72180620623172,1.73760405655992,
1.74021654151974,1.74156242637286,1.74263379570719,1.74389198546095,1.74617210055741,
1.75760866774367,1.78402402434625,1.83638785826709,1.84332628653457,1.84620036353465,
1.84799482292824,1.84995543205559,1.85265695163944,1.85904680944289,1.8873851252852,
1.93728518809846,1.94991467480724,1.9521509073944,1.95353452565234,1.95460903332621,
1.95584057180149,1.95799878626154,1.9675076620991,2.0166420977235,2.0518281950266,
2.05612455429066,2.05866631607403,2.0606073214597,2.06268087157703,2.06592968561963,
2.07623891824444,2.09279809288288,2.12568565576995,2.13955224267007,2.14611373514652,
2.16166408012244,2.16426452422766,2.16560776704704,2.16667891902104,2.16793904706968,
2.17022829108759,2.18182886955132,2.20890471931824,2.26033650400616,2.26733516463324,
2.2702191034823,2.2720152946656,2.27397426243379,2.2766670833449,2.28300627268811,
2.31092526152792,2.35694144007021,2.35793644658125,2.37366886787483,2.37627707080484,
2.37762198667344,2.37869323812628,2.3799520485334,2.38223522731371,2.39372765743041,
2.42036726017418,2.47238397040264,2.4793619331355,2.48224243562505,2.48403799251657,
2.48585857696639,2.48841312006702,2.49401415860211,2.5015383928661,2.52051152887596,
2.54851967678728,2.58534455777052,2.58818633431194,2.58956083432058,2.59063435158216,
2.59187164123774,2.59405640205728,2.6039529815351,2.65275133922535,2.66750913583394),
 .UNSPECIFIED.);
#1861=B_SPLINE_CURVE_WITH_KNOTS('',3,(#178521,#178522,#178523,#178524,#178525,
#178526,#178527,#178528,#178529,#178530,#178531,#178532,#178533,#178534,
#178535,#178536,#178537,#178538,#178539,#178540,#178541,#178542),
 .UNSPECIFIED.,.F.,.F.,(4,2,2,2,2,2,2,2,2,2,4),(0.000768648173035884,0.0217309694116398,
0.024834106463169,0.0269704254108821,0.0287696705621352,0.0306848619248692,
0.0330687977058306,0.0367500448424231,0.0545887128832821,0.0729754669855961,
0.0751664112996189),.UNSPECIFIED.);
#1862=B_SPLINE_CURVE_WITH_KNOTS('',3,(#178547,#178548,#178549,#178550,#178551,
#178552,#178553,#178554,#178555,#178556,#178557,#178558,#178559,#178560,
#178561,#178562,#178563,#178564,#178565,#178566,#178567,#178568,#178569,
#178570,#178571,#178572,#178573,#178574,#178575,#178576,#178577,#178578,
#178579,#178580,#178581,#178582,#178583,#178584,#178585,#178586,#178587,
#178588,#178589,#178590,#178591,#178592,#178593,#178594,#178595,#178596,
#178597,#178598,#178599,#178600,#178601,#178602,#178603,#178604,#178605,
#178606,#178607,#178608,#178609,#178610,#178611,#178612,#178613,#178614,
#178615,#178616,#178617,#178618,#178619,#178620,#178621,#178622,#178623,
#178624,#178625,#178626,#178627,#178628,#178629,#178630,#178631,#178632,
#178633,#178634,#178635,#178636,#178637,#178638,#178639,#178640,#178641,
#178642,#178643,#178644,#178645,#178646,#178647,#178648,#178649,#178650,
#178651,#178652,#178653,#178654,#178655,#178656,#178657,#178658,#178659,
#178660,#178661,#178662,#178663,#178664,#178665,#178666,#178667,#178668,
#178669,#178670,#178671,#178672,#178673,#178674,#178675,#178676,#178677,
#178678,#178679,#178680,#178681,#178682,#178683,#178684,#178685,#178686,
#178687,#178688,#178689,#178690,#178691,#178692,#178693,#178694,#178695,
#178696,#178697,#178698,#178699,#178700,#178701,#178702,#178703,#178704,
#178705,#178706,#178707,#178708,#178709,#178710,#178711,#178712,#178713,
#178714,#178715,#178716,#178717,#178718,#178719,#178720,#178721,#178722,
#178723,#178724,#178725,#178726,#178727,#178728,#178729,#178730,#178731,
#178732,#178733,#178734,#178735,#178736,#178737,#178738,#178739,#178740,
#178741,#178742,#178743,#178744,#178745,#178746,#178747,#178748,#178749,
#178750,#178751,#178752,#178753,#178754,#178755,#178756,#178757,#178758,
#178759,#178760,#178761,#178762,#178763,#178764,#178765,#178766,#178767,
#178768,#178769,#178770,#178771,#178772,#178773,#178774,#178775,#178776,
#178777,#178778),.UNSPECIFIED.,.F.,.F.,(4,2,2,2,2,2,2,2,2,2,2,2,2,2,2,2,
2,2,2,2,2,2,2,2,2,2,2,2,2,2,2,2,2,2,2,2,2,2,2,2,2,2,2,2,2,2,2,2,2,2,2,2,
2,2,2,2,2,2,2,2,2,2,2,2,2,2,2,2,2,2,2,2,2,2,2,2,2,2,2,2,2,2,2,2,2,2,2,2,
2,2,2,2,2,2,2,2,2,2,2,2,2,2,2,2,2,2,2,2,2,2,2,2,2,2,2,4),(1.25995284018407,
1.27815533267849,1.30765697349692,1.31206706936864,1.31439383091612,1.31612079616701,
1.31827707165333,1.32189964021149,1.33434948216398,1.38530655022404,1.41651402911594,
1.41942699928209,1.42081555372547,1.42189061163399,1.42311910645899,1.42526335265726,
1.43457548440155,1.48373090332537,1.5191186820702,1.52341772045822,1.52596031999528,
1.52790153498849,1.5299748921498,1.53322253386872,1.54352072105679,1.56005519322258,
1.59292311329251,1.60444895088282,1.61420015696443,1.61610257435304,1.62916930768846,
1.63142803064148,1.63281839164975,1.6338935711981,1.6351207785474,1.63725944359352,
1.64649611756226,1.665155557615,1.70929886538824,1.73174157288586,1.73568379926241,
1.73814776146543,1.74007158146695,1.74220153389174,1.74570551189524,1.75848205950185,
1.78092536766237,1.80819133767747,1.84051393284874,1.84341562564243,1.84480190532759,
1.84587663413865,1.84710635726372,1.84925651592167,1.85865301629504,1.90788222371777,
1.94309504594036,1.94739154272531,1.94993327551323,1.95187419521534,1.95394759220047,
1.95719603772935,1.96750301755928,1.9840575435563,2.0169402232118,2.05257689975077,
2.05544010149944,2.05681883306758,2.05789277623411,2.0591273087319,2.0612994304239,
2.07100980878776,2.11996641100843,2.15509560822262,2.15939088810079,2.16193222222516,
2.16387302250177,2.16594647128081,2.16919537246461,2.17950695458013,2.19607187559424,
2.2289625194241,2.26456745940368,2.26743324883355,2.26881245849163,2.26988641435369,
2.27112055597793,2.27329102320292,2.28297817945522,2.33195248070879,2.36708663309277,
2.37138184122927,2.37392310835603,2.37586384332775,2.37793720862947,2.38118595038636,
2.39149678517998,2.40806027606265,2.47069227330701,2.47205345242812,2.47822624636479,
2.48016435853052,2.48134700118584,2.48237852780508,2.48379140889466,2.48680603945378,
2.4909036416418,2.50118056489532,2.52399975601406,2.57570490377446,2.58268778886798,
2.58556926597903,2.58736511868518,2.58932467119699,2.59202003277444,2.59362475265785),
 .UNSPECIFIED.);
#1863=B_SPLINE_CURVE_WITH_KNOTS('',3,(#178779,#178780,#178781,#178782,#178783,
#178784,#178785,#178786,#178787,#178788,#178789,#178790,#178791,#178792,
#178793,#178794,#178795,#178796,#178797,#178798,#178799,#178800,#178801,
#178802,#178803,#178804,#178805,#178806,#178807,#178808,#178809,#178810,
#178811,#178812,#178813,#178814,#178815,#178816,#178817,#178818,#178819,
#178820,#178821,#178822,#178823,#178824,#178825,#178826,#178827,#178828,
#178829,#178830,#178831,#178832,#178833,#178834,#178835,#178836,#178837,
#178838,#178839,#178840,#178841,#178842,#178843,#178844,#178845,#178846,
#178847,#178848,#178849,#178850,#178851,#178852,#178853,#178854,#178855,
#178856,#178857,#178858,#178859,#178860,#178861,#178862,#178863,#178864,
#178865,#178866,#178867,#178868,#178869,#178870,#178871,#178872,#178873,
#178874,#178875,#178876,#178877,#178878,#178879,#178880,#178881,#178882,
#178883,#178884,#178885,#178886,#178887,#178888,#178889,#178890,#178891,
#178892,#178893,#178894,#178895,#178896,#178897,#178898,#178899,#178900,
#178901,#178902,#178903,#178904,#178905,#178906,#178907,#178908,#178909,
#178910,#178911,#178912,#178913,#178914,#178915,#178916,#178917,#178918,
#178919,#178920,#178921,#178922,#178923,#178924,#178925,#178926,#178927,
#178928,#178929,#178930,#178931,#178932,#178933,#178934,#178935,#178936,
#178937,#178938,#178939,#178940,#178941,#178942,#178943,#178944,#178945,
#178946,#178947,#178948,#178949,#178950,#178951,#178952,#178953,#178954,
#178955,#178956,#178957,#178958,#178959,#178960,#178961,#178962,#178963,
#178964,#178965,#178966,#178967,#178968,#178969,#178970,#178971,#178972,
#178973,#178974,#178975,#178976,#178977,#178978,#178979,#178980,#178981,
#178982,#178983,#178984,#178985,#178986,#178987,#178988,#178989,#178990,
#178991,#178992,#178993,#178994,#178995,#178996,#178997,#178998,#178999,
#179000,#179001,#179002,#179003,#179004,#179005,#179006,#179007,#179008,
#179009,#179010,#179011,#179012),.UNSPECIFIED.,.F.,.F.,(4,2,2,2,2,2,2,2,
2,2,2,2,2,2,2,2,2,2,2,2,2,2,2,2,2,2,2,2,2,2,2,2,2,2,2,2,2,2,2,2,2,2,2,2,
2,2,2,2,2,2,2,2,2,2,2,2,2,2,2,2,2,2,2,2,2,2,2,2,2,2,2,2,2,2,2,2,2,2,2,2,
2,2,2,2,2,2,2,2,2,2,2,2,2,2,2,2,2,2,2,2,2,2,2,2,2,2,2,2,2,2,2,2,2,2,2,2,
4),(0.0751664112996189,0.121836951464716,0.131681142658904,0.133862213611629,
0.135098605469386,0.136172108887128,0.137547580294155,0.14039476577867,
0.176868086307239,0.2094289106163,0.225633610738257,0.232378429874515,0.237517855736887,
0.239980375628617,0.241821624375069,0.24364900313207,0.246193616401099,
0.252852140385327,0.308506881526599,0.332697523544293,0.343554680832648,
0.345800707706044,0.347051384853921,0.348123287830775,0.349478711949654,
0.351622237597027,0.362626672188654,0.413890619380091,0.442557303123207,
0.448986537823899,0.451694527804662,0.453656137297877,0.455448972236416,
0.458314902646815,0.46520498464097,0.518242956848075,0.544209029002317,
0.555530797239845,0.557804212089946,0.559060861729059,0.560132231379342,
0.561479779883051,0.564100380196642,0.580124489072943,0.585201163504066,
0.629881790974561,0.648403612356206,0.659578923632395,0.662923321289518,
0.665017807074267,0.666950981328522,0.669443797604298,0.67357288603625,
0.700868461682789,0.74311955698701,0.759406575996171,0.767853917475503,
0.769932099700476,0.771145854515035,0.77222353355997,0.773612688327964,
0.775917681979813,0.78992994807999,0.791300118797791,0.798313753017245,
0.811988337896586,0.844849351005156,0.861410889239503,0.871722134906194,
0.874971107247304,0.877044650403876,0.878985573955134,0.881527121121702,
0.885822908864002,0.920955317153874,0.969901905753939,0.979660705440998,
0.98183631026648,0.983071676473829,0.984145615712196,0.98552337908981,0.988381266748878,
1.01124170619927,1.02400669700314,1.05686244962613,1.07341519158678,1.0837227575136,
1.08697152696743,1.08904517055803,1.09098634964885,1.09352846452316,1.09782573434743,
1.13304047916014,1.18224589934266,1.19170985783632,1.1938650800132,1.19509604121575,
1.19617078239087,1.19755566047973,1.19979579975946,1.21249724873201,1.23487540300981,
1.2684790562292,1.2938562858841,1.29812699327806,1.30042452759205,1.30231760049,
1.30455834645752,1.3084575115031,1.32436621650597,1.3345884751666,1.37387287669931,
1.40245709623738,1.40536965373442,1.40675820520218,1.40783335001672,1.40876523686012),
 .UNSPECIFIED.);
#1864=B_SPLINE_CURVE_WITH_KNOTS('',3,(#179018,#179019,#179020,#179021,#179022,
#179023,#179024,#179025,#179026,#179027,#179028,#179029,#179030,#179031,
#179032,#179033,#179034,#179035,#179036,#179037,#179038,#179039),
 .UNSPECIFIED.,.F.,.F.,(4,2,2,2,2,2,2,2,2,2,4),(2.5930073351113,2.59655707612435,
2.60120237925256,2.60293217092639,2.60395546436,2.6050492651463,2.60656781487107,
2.61019870485997,2.6153096210448,2.62947688779406,2.66710874015144),
 .UNSPECIFIED.);
#1865=B_SPLINE_CURVE_WITH_KNOTS('',3,(#179040,#179041,#179042,#179043,#179044,
#179045,#179046,#179047,#179048,#179049,#179050,#179051,#179052,#179053,
#179054,#179055,#179056,#179057,#179058,#179059,#179060,#179061,#179062,
#179063,#179064,#179065,#179066,#179067,#179068,#179069,#179070,#179071,
#179072,#179073,#179074,#179075,#179076,#179077,#179078,#179079,#179080,
#179081,#179082,#179083,#179084,#179085,#179086,#179087,#179088,#179089,
#179090,#179091,#179092,#179093,#179094,#179095,#179096,#179097,#179098,
#179099,#179100,#179101,#179102,#179103,#179104,#179105,#179106,#179107,
#179108,#179109,#179110,#179111,#179112,#179113,#179114,#179115,#179116,
#179117,#179118,#179119,#179120,#179121,#179122,#179123,#179124,#179125,
#179126,#179127,#179128,#179129,#179130,#179131,#179132,#179133,#179134,
#179135,#179136,#179137,#179138,#179139,#179140,#179141,#179142,#179143,
#179144,#179145,#179146,#179147,#179148,#179149,#179150,#179151,#179152,
#179153,#179154,#179155,#179156,#179157,#179158,#179159,#179160,#179161,
#179162,#179163,#179164,#179165,#179166,#179167,#179168,#179169,#179170,
#179171,#179172,#179173,#179174,#179175,#179176,#179177,#179178,#179179,
#179180,#179181,#179182,#179183,#179184,#179185,#179186,#179187,#179188,
#179189,#179190,#179191,#179192,#179193,#179194,#179195,#179196,#179197,
#179198,#179199,#179200,#179201,#179202,#179203,#179204,#179205,#179206,
#179207,#179208,#179209,#179210,#179211,#179212,#179213,#179214,#179215,
#179216,#179217,#179218,#179219,#179220,#179221,#179222,#179223,#179224,
#179225,#179226,#179227,#179228,#179229,#179230,#179231,#179232,#179233,
#179234,#179235,#179236,#179237,#179238,#179239,#179240,#179241,#179242,
#179243,#179244,#179245,#179246,#179247,#179248,#179249,#179250,#179251,
#179252,#179253,#179254,#179255,#179256,#179257,#179258,#179259,#179260,
#179261,#179262,#179263),.UNSPECIFIED.,.F.,.F.,(4,2,2,2,2,2,2,2,2,2,2,2,
2,2,2,2,2,2,2,2,2,2,2,2,2,2,2,2,2,2,2,2,2,2,2,2,2,2,2,2,2,2,2,2,2,2,2,2,
2,2,2,2,2,2,2,2,2,2,2,2,2,2,2,2,2,2,2,2,2,2,2,2,2,2,2,2,2,2,2,2,2,2,2,2,
2,2,2,2,2,2,2,2,2,2,2,2,2,2,2,2,2,2,2,2,2,2,2,2,2,2,2,4),(0.000704174783266484,
0.0257175604482853,0.0359848121210841,0.0390635446877278,0.0411898447752388,
0.0432709978131024,0.0452083577367602,0.0477299553379147,0.0519581062662032,
0.0833496643500498,0.108683991109725,0.136591220283264,0.145906684913021,
0.148050668850133,0.149278836543247,0.150353498249269,0.151741385255173,
0.154652423469552,0.186428100892679,0.237019928806342,0.245245998359551,
0.251260637921565,0.253888587904228,0.255845177211792,0.257643302003301,
0.260539405344161,0.267613575549391,0.317990518515176,0.355630100276971,
0.359217020733819,0.360727971305265,0.361820314740776,0.362845441579523,
0.364585128297621,0.369296593408011,0.409885702767462,0.456766765021495,
0.463159531935094,0.465861115581181,0.467821348318664,0.469615175354509,
0.472487599269587,0.479418712975679,0.53187624579876,0.55823965171709,0.569661293388527,
0.571940169362427,0.573197891653986,0.574268997283979,0.575614715574956,
0.578227361376873,0.594085310341687,0.598886501397849,0.614100754358038,
0.646973648978801,0.663553423044398,0.673872438409335,0.677121953267134,
0.679195385113979,0.681135883172054,0.683676409714467,0.6879694338944,0.730360837973206,
0.75940491758315,0.774136636136039,0.782031822114532,0.784063874694209,
0.785267280880008,0.786347264976097,0.78775444750052,0.790121315900346,
0.805548432964546,0.812282711181535,0.826072038655682,0.858930118198779,
0.87549101521074,0.885801617049223,0.88905025645457,0.891123555881361,0.893064229345933,
0.895605417375026,0.899900527140571,0.935018038083059,0.983926479072149,
0.993721999751709,0.995899923745845,0.997135704694492,0.99820942740478,
0.999586159067221,1.00243931456665,1.02512119130855,1.03806228554941,1.0709155347101,
1.08746815996987,1.09777531880078,1.10102378197149,1.10309718729489,1.10503811329192,
1.10757985336449,1.11187639242141,1.14707193209009,1.19622157390507,1.20574153761124,
1.20790053021267,1.20913222685479,1.2102066928978,1.21159001138132,1.2138252679769,
1.22643731494536,1.23296338685451,1.2380952997305,1.25995284018407),
 .UNSPECIFIED.);
#1866=B_SPLINE_CURVE_WITH_KNOTS('',3,(#179265,#179266,#179267,#179268,#179269,
#179270,#179271,#179272,#179273,#179274,#179275,#179276,#179277,#179278,
#179279,#179280,#179281,#179282,#179283,#179284,#179285,#179286,#179287,
#179288,#179289,#179290,#179291,#179292,#179293,#179294,#179295,#179296,
#179297,#179298,#179299,#179300,#179301,#179302,#179303,#179304,#179305,
#179306,#179307,#179308,#179309,#179310,#179311,#179312,#179313,#179314,
#179315,#179316,#179317,#179318,#179319,#179320,#179321,#179322,#179323,
#179324,#179325,#179326,#179327,#179328,#179329,#179330,#179331,#179332,
#179333,#179334,#179335,#179336,#179337,#179338,#179339,#179340,#179341,
#179342,#179343,#179344,#179345,#179346,#179347,#179348,#179349,#179350,
#179351,#179352,#179353,#179354,#179355,#179356,#179357,#179358,#179359,
#179360,#179361,#179362,#179363,#179364,#179365,#179366,#179367,#179368,
#179369,#179370,#179371,#179372,#179373,#179374,#179375,#179376,#179377,
#179378,#179379,#179380,#179381,#179382,#179383,#179384,#179385,#179386,
#179387,#179388,#179389,#179390,#179391,#179392,#179393,#179394,#179395,
#179396,#179397,#179398,#179399,#179400,#179401,#179402,#179403,#179404,
#179405,#179406,#179407,#179408,#179409,#179410,#179411,#179412,#179413,
#179414,#179415,#179416,#179417,#179418,#179419,#179420,#179421,#179422,
#179423,#179424,#179425,#179426,#179427,#179428,#179429,#179430,#179431,
#179432,#179433,#179434,#179435,#179436,#179437,#179438,#179439,#179440,
#179441,#179442,#179443,#179444,#179445,#179446,#179447,#179448,#179449,
#179450,#179451,#179452,#179453,#179454,#179455,#179456,#179457,#179458,
#179459,#179460,#179461,#179462,#179463,#179464,#179465,#179466,#179467,
#179468,#179469,#179470,#179471,#179472,#179473,#179474,#179475,#179476,
#179477,#179478,#179479,#179480,#179481,#179482,#179483,#179484,#179485,
#179486,#179487,#179488,#179489,#179490,#179491,#179492,#179493,#179494,
#179495,#179496,#179497,#179498,#179499,#179500,#179501,#179502,#179503,
#179504,#179505,#179506,#179507,#179508,#179509,#179510,#179511,#179512,
#179513,#179514,#179515,#179516,#179517,#179518,#179519,#179520),
 .UNSPECIFIED.,.F.,.F.,(4,2,2,2,2,2,2,2,2,2,2,2,2,2,2,2,2,2,2,2,2,2,2,2,
2,2,2,2,2,2,2,2,2,2,2,2,2,2,2,2,2,2,2,2,2,2,2,2,2,2,2,2,2,2,2,2,2,2,2,2,
2,2,2,2,2,2,2,2,2,2,2,2,2,2,2,2,2,2,2,2,2,2,2,2,2,2,2,2,2,2,2,2,2,2,2,2,
2,2,2,2,2,2,2,2,2,2,2,2,2,2,2,2,2,2,2,2,2,2,2,2,2,2,2,2,2,2,2,4),(1.40876523686012,
1.40906204393765,1.41120687144366,1.42052514418392,1.46970161844819,1.50507081289879,
1.50936999286094,1.51191275499292,1.51385413951598,1.51592772173571,1.51917580776507,
1.52947617622816,1.54601488419058,1.57356168633321,1.58970408754065,1.60078465259348,
1.6150205401593,1.6173371712821,1.6187298593166,1.61980813782155,1.62102018173609,
1.62309009026263,1.6314324540752,1.6474136860404,1.68972792942271,1.71734566106792,
1.72148338727517,1.72397897743458,1.72591284550596,1.72800662795603,1.73134675056564,
1.74247827516818,1.76089964199186,1.80770817811134,1.81253297817898,1.82701627756262,
1.82934425026303,1.83074028129115,1.83181901714088,1.83302919573545,1.83509063606512,
1.84332931772284,1.85901491237136,1.90092755750791,1.92932631736605,1.93348475129867,
1.9359864464662,1.93792127381585,1.94001234369268,1.94334004829138,1.95435551753042,
1.97250823563918,2.02218424317245,2.02373330487373,2.02563794733054,2.03913289798561,
2.04141316979618,2.04279519462395,2.04387218595884,2.04509064120281,2.04718924198271,
2.05589101581214,2.07291936302207,2.11593620512401,2.1282171496421,2.14272193700362,
2.14650164868605,2.14871489652755,2.15062763117179,2.1529657335204,2.1574291941509,
2.18882831143217,2.23938702440558,2.25132987941368,2.25352918546455,2.25490178413962,
2.25597541182666,2.25721463742382,2.25940718010277,2.26941316893368,2.31813785790198,
2.35319435175552,2.3574897097279,2.36003142069175,2.36197269920623,2.36404684359362,
2.36729722041653,2.37761673872991,2.39419750467077,2.4279021680599,2.46267411909094,
2.46555349924636,2.46693559163019,2.46797846857451,2.46798322666971,2.46798790131232,
2.46799249431981,2.46799700757368,2.46800144279414,2.46800580147029,2.4680100855505,
2.46801429655875,2.46801843592317,2.46802250542493,2.46802650641665,2.46803044037086,
2.46803430867444,2.46803790597397,2.4680414897071,2.46804506013325,2.4680486173852,
2.46805216134702,2.4692761030427,2.47058782654189,2.4726125604927,2.4764297583911,
2.48571877521554,2.52371378071088,2.53834977058261,2.5655065850755,2.56963265583248,
2.5721249092442,2.57405838426332,2.57615393187958,2.57950162033336,2.59070276111532,
2.60928557013674,2.66833801738852),.UNSPECIFIED.);
#1867=B_SPLINE_CURVE_WITH_KNOTS('',3,(#179521,#179522,#179523,#179524,#179525,
#179526,#179527,#179528,#179529,#179530,#179531,#179532,#179533,#179534,
#179535,#179536,#179537,#179538,#179539,#179540,#179541,#179542),
 .UNSPECIFIED.,.F.,.F.,(4,2,2,2,2,2,2,2,2,2,4),(0.000810717437210857,0.00554260819479371,
0.00881068906929704,0.0102445691543466,0.0113189779225148,0.0123417943062969,
0.013364996033305,0.0148060118696489,0.0186526098088544,0.02639099987356,
0.0750462537154924),.UNSPECIFIED.);
#1868=B_SPLINE_CURVE_WITH_KNOTS('',3,(#179547,#179548,#179549,#179550,#179551,
#179552,#179553,#179554,#179555,#179556,#179557,#179558,#179559,#179560,
#179561,#179562,#179563,#179564,#179565,#179566,#179567,#179568,#179569,
#179570,#179571,#179572,#179573,#179574,#179575,#179576,#179577,#179578,
#179579,#179580,#179581,#179582,#179583,#179584,#179585,#179586,#179587,
#179588,#179589,#179590,#179591,#179592,#179593,#179594,#179595,#179596,
#179597,#179598,#179599,#179600,#179601,#179602,#179603,#179604,#179605,
#179606,#179607,#179608,#179609,#179610,#179611,#179612,#179613,#179614,
#179615,#179616,#179617,#179618,#179619,#179620,#179621,#179622,#179623,
#179624,#179625,#179626,#179627,#179628,#179629,#179630,#179631,#179632,
#179633,#179634,#179635,#179636,#179637,#179638,#179639,#179640,#179641,
#179642,#179643,#179644,#179645,#179646,#179647,#179648,#179649,#179650,
#179651,#179652,#179653,#179654,#179655,#179656,#179657,#179658,#179659,
#179660,#179661,#179662,#179663,#179664,#179665,#179666,#179667,#179668,
#179669,#179670,#179671,#179672,#179673,#179674,#179675,#179676,#179677,
#179678,#179679,#179680,#179681,#179682,#179683,#179684,#179685,#179686,
#179687,#179688,#179689,#179690,#179691,#179692,#179693,#179694,#179695,
#179696,#179697,#179698,#179699,#179700,#179701,#179702,#179703,#179704,
#179705,#179706,#179707,#179708,#179709,#179710,#179711,#179712,#179713,
#179714,#179715,#179716,#179717,#179718,#179719,#179720,#179721,#179722,
#179723,#179724,#179725,#179726,#179727,#179728,#179729,#179730,#179731,
#179732,#179733,#179734,#179735,#179736,#179737,#179738,#179739,#179740,
#179741,#179742,#179743,#179744,#179745,#179746,#179747,#179748,#179749,
#179750,#179751,#179752,#179753,#179754,#179755,#179756,#179757,#179758,
#179759,#179760,#179761,#179762,#179763,#179764,#179765,#179766,#179767,
#179768,#179769,#179770,#179771,#179772,#179773,#179774,#179775,#179776),
 .UNSPECIFIED.,.F.,.F.,(4,2,2,2,2,2,2,2,2,2,2,2,2,2,2,2,2,2,2,2,2,2,2,2,
2,2,2,2,2,2,2,2,2,2,2,2,2,2,2,2,2,2,2,2,2,2,2,2,2,2,2,2,2,2,2,2,2,2,2,2,
2,2,2,2,2,2,2,2,2,2,2,2,2,2,2,2,2,2,2,2,2,2,2,2,2,2,2,2,2,2,2,2,2,2,2,2,
2,2,2,2,2,2,2,2,2,2,2,2,2,2,2,2,2,2,4),(1.25952994513294,1.26421488598236,
1.30515481544145,1.32763223119784,1.33029538162279,1.33163408266925,1.33260195983659,
1.33382544749752,1.33594775047286,1.34496553108,1.36294881533076,1.41315940227977,
1.4309613348525,1.43464041070228,1.43702379248317,1.43893908622121,1.44111762204123,
1.44484207719109,1.46024701804637,1.51157709626072,1.53925268004026,1.54215933447374,
1.54354650258749,1.54462123616883,1.54585019886904,1.54799722878005,1.55735197908928,
1.60661243391117,1.64183221861147,1.64612844434328,1.64866997749064,1.6506107221197,
1.65268391015098,1.65593198252428,1.66623739265292,1.68278903068098,1.71566752358765,
1.72911330028546,1.736696610636,1.75169296612739,1.75404224757913,1.75544430252706,
1.75652358368923,1.75772980714153,1.75977446645524,1.76781718180068,1.78295449543262,
1.82265124657729,1.8538880913086,1.85811304970662,1.86063381774351,1.86257115604171,
1.8646528892407,1.86794005869551,1.87859162512038,1.89591648917634,1.94411119254616,
1.9484064128245,1.95083887569047,1.96382573538939,1.96608014904842,1.96746910199456,
1.9685439839178,1.96977173596555,1.97191341784866,1.98119485777428,1.99999636799541,
2.04034065568394,2.05258399045552,2.06729683600943,2.07109426502402,2.07331120119358,
2.07522308690815,2.07755508258722,2.08199131224631,2.11242019220516,2.15453760179427,
2.15952788394103,2.17553328083814,2.17815268663513,2.17949994613809,2.18057125656893,
2.18182804021792,2.18410220413738,2.19543864623566,2.22146059245618,2.27437230825323,
2.28126892435235,2.28413586067807,2.28592883098994,2.28789019755062,2.29059712748133,
2.29702039834854,2.30588627237321,2.35712846618111,2.3871381137356,2.39005251520849,
2.39144118007698,2.39251606035343,2.39374405795638,2.39588674731219,2.40518147929141,
2.42402448743626,2.47021464779431,2.47167402645945,2.4906970588245,2.49445667183905,
2.49686485014865,2.49878240296042,2.50057963286904,2.50367219632359,2.51321649453698,
2.52821612536213,2.55050832517838,2.5930073351113),.UNSPECIFIED.);
#1869=B_SPLINE_CURVE_WITH_KNOTS('',3,(#179777,#179778,#179779,#179780,#179781,
#179782,#179783,#179784,#179785,#179786,#179787,#179788,#179789,#179790,
#179791,#179792,#179793,#179794,#179795,#179796,#179797,#179798,#179799,
#179800,#179801,#179802,#179803,#179804,#179805,#179806,#179807,#179808,
#179809,#179810,#179811,#179812,#179813,#179814,#179815,#179816,#179817,
#179818,#179819,#179820,#179821,#179822,#179823,#179824,#179825,#179826,
#179827,#179828,#179829,#179830,#179831,#179832,#179833,#179834,#179835,
#179836,#179837,#179838,#179839,#179840,#179841,#179842,#179843,#179844,
#179845,#179846,#179847,#179848,#179849,#179850,#179851,#179852,#179853,
#179854,#179855,#179856,#179857,#179858,#179859,#179860,#179861,#179862,
#179863,#179864,#179865,#179866,#179867,#179868,#179869,#179870,#179871,
#179872,#179873,#179874,#179875,#179876,#179877,#179878,#179879,#179880,
#179881,#179882,#179883,#179884,#179885,#179886,#179887,#179888,#179889,
#179890,#179891,#179892,#179893,#179894,#179895,#179896,#179897,#179898,
#179899,#179900,#179901,#179902,#179903,#179904,#179905,#179906,#179907,
#179908,#179909,#179910,#179911,#179912,#179913,#179914,#179915,#179916,
#179917,#179918,#179919,#179920,#179921,#179922,#179923,#179924,#179925,
#179926,#179927,#179928,#179929,#179930,#179931,#179932,#179933,#179934,
#179935,#179936,#179937,#179938,#179939,#179940,#179941,#179942,#179943,
#179944,#179945,#179946,#179947,#179948,#179949,#179950,#179951,#179952,
#179953,#179954,#179955,#179956,#179957,#179958,#179959,#179960,#179961,
#179962,#179963,#179964,#179965,#179966,#179967,#179968,#179969,#179970,
#179971,#179972,#179973,#179974,#179975,#179976,#179977,#179978,#179979,
#179980,#179981,#179982,#179983,#179984,#179985,#179986,#179987,#179988,
#179989,#179990,#179991,#179992,#179993,#179994,#179995,#179996,#179997,
#179998,#179999,#180000,#180001,#180002,#180003,#180004,#180005,#180006,
#180007,#180008,#180009,#180010,#180011,#180012),.UNSPECIFIED.,.F.,.F.,
(4,2,2,2,2,2,2,2,2,2,2,2,2,2,2,2,2,2,2,2,2,2,2,2,2,2,2,2,2,2,2,2,2,2,2,
2,2,2,2,2,2,2,2,2,2,2,2,2,2,2,2,2,2,2,2,2,2,2,2,2,2,2,2,2,2,2,2,2,2,2,2,
2,2,2,2,2,2,2,2,2,2,2,2,2,2,2,2,2,2,2,2,2,2,2,2,2,2,2,2,2,2,2,2,2,2,2,2,
2,2,2,2,2,2,2,2,2,2,4),(0.0750462537154924,0.0761256387381507,0.0989704599401781,
0.111902023384075,0.115419514704814,0.117551996243827,0.119474442395931,
0.121931582678128,0.125852746736523,0.147816198389106,0.207378558798831,
0.215844141380436,0.219418647549753,0.221351067985563,0.222624367089238,
0.22381832530777,0.22486186355796,0.226241575681799,0.229110441793543,0.264441139330251,
0.297386333548054,0.320271350619973,0.325968993619703,0.328548272074073,
0.330487894856251,0.332312144273875,0.334844970402375,0.34142889523907,
0.397818524492796,0.421525799092587,0.432252016242608,0.434490053279475,
0.43573897705894,0.436811042889057,0.438168812213042,0.440837179037049,
0.458109395767358,0.506984886462512,0.525221604404314,0.536273817059415,
0.539604938382228,0.541696425940234,0.543630459272732,0.546129470483122,
0.550279867378455,0.578398283385265,0.620497966164504,0.636274838914577,
0.644544264374919,0.646607926012674,0.647818420132488,0.648896767101814,
0.650291410266022,0.652615204121303,0.667014290583278,0.675576461617543,
0.688666349578805,0.721520054295096,0.744258604835183,0.749936812927187,
0.752512694959083,0.754451951899493,0.756277460950942,0.75881460231764,
0.765424704729817,0.821578218729879,0.8454455735475,0.856215800686848,0.858456695258177,
0.859706322545346,0.8607784416626,0.862135571516215,0.864800557564629,0.881974431453238,
0.927477837906839,0.955339008804063,0.961671787050835,0.964363585663553,
0.96632243793558,0.968118962517457,0.97100438967605,0.978011517918973,1.02935530668646,
1.05652792900927,1.06815196686868,1.07044262972475,1.07170310267479,1.07277428874515,
1.07411724023462,1.07671614900153,1.09222950274384,1.09880436863915,1.14018857818637,
1.16745745311394,1.17371819061984,1.17639772089854,1.17835445569228,1.18015378074087,
1.18305417638074,1.19015070267775,1.23978682627901,1.27816935568051,1.28175573391504,
1.28326688406574,1.28435953159511,1.28538507100967,1.28712572923928,1.29184140475802,
1.33225690507557,1.33414658502961,1.37797807156991,1.38520107324248,1.38812273809624,
1.38992601791968,1.39187979227601,1.3945422296185,1.40070386231283,1.40864677202052),
 .UNSPECIFIED.);
#1870=B_SPLINE_CURVE_WITH_KNOTS('',3,(#180018,#180019,#180020,#180021),
 .UNSPECIFIED.,.F.,.F.,(4,4),(152.105783788367,152.455231354966),
 .UNSPECIFIED.);
#1871=B_SPLINE_CURVE_WITH_KNOTS('',3,(#180022,#180023,#180024,#180025,#180026,
#180027,#180028,#180029,#180030,#180031,#180032,#180033,#180034,#180035,
#180036,#180037,#180038,#180039,#180040,#180041,#180042,#180043,#180044,
#180045,#180046,#180047,#180048,#180049,#180050,#180051,#180052,#180053,
#180054,#180055,#180056,#180057,#180058,#180059,#180060,#180061,#180062,
#180063,#180064,#180065,#180066,#180067,#180068,#180069,#180070,#180071,
#180072,#180073,#180074,#180075,#180076,#180077,#180078,#180079,#180080,
#180081,#180082,#180083,#180084,#180085,#180086,#180087,#180088,#180089,
#180090,#180091,#180092,#180093,#180094,#180095,#180096,#180097,#180098,
#180099,#180100,#180101,#180102,#180103,#180104,#180105,#180106,#180107,
#180108,#180109,#180110,#180111,#180112,#180113,#180114,#180115,#180116,
#180117,#180118,#180119,#180120,#180121,#180122,#180123,#180124,#180125,
#180126,#180127,#180128,#180129,#180130,#180131,#180132,#180133,#180134,
#180135,#180136,#180137,#180138,#180139,#180140,#180141,#180142,#180143,
#180144,#180145,#180146,#180147,#180148,#180149,#180150,#180151,#180152,
#180153,#180154,#180155,#180156,#180157,#180158,#180159,#180160,#180161,
#180162,#180163,#180164,#180165,#180166,#180167,#180168,#180169,#180170,
#180171,#180172,#180173,#180174,#180175,#180176,#180177,#180178,#180179,
#180180,#180181,#180182,#180183,#180184,#180185,#180186,#180187,#180188,
#180189,#180190,#180191,#180192,#180193,#180194,#180195,#180196,#180197,
#180198,#180199,#180200,#180201,#180202,#180203,#180204,#180205,#180206,
#180207,#180208,#180209,#180210,#180211,#180212,#180213,#180214,#180215,
#180216,#180217,#180218,#180219,#180220,#180221,#180222,#180223,#180224,
#180225,#180226,#180227,#180228,#180229,#180230,#180231,#180232,#180233,
#180234,#180235,#180236,#180237,#180238,#180239,#180240,#180241,#180242,
#180243,#180244,#180245,#180246,#180247),.UNSPECIFIED.,.F.,.F.,(4,2,2,2,
2,2,2,2,2,2,2,2,2,2,2,2,2,2,2,2,2,2,2,2,2,2,2,2,2,2,2,2,2,2,2,2,2,2,2,2,
2,2,2,2,2,2,2,2,2,2,2,2,2,2,2,2,2,2,2,2,2,2,2,2,2,2,2,2,2,2,2,2,2,2,2,2,
2,2,2,2,2,2,2,2,2,2,2,2,2,2,2,2,2,2,2,2,2,2,2,2,2,2,2,2,2,2,2,2,2,2,2,2,
4),(0.000629316459415605,0.0219107407500348,0.0544690400356165,0.058013446133146,
0.0595170939913138,0.0606081537861777,0.0616352682843622,0.0633851800392661,
0.0681640862994912,0.104196691217396,0.118264876043651,0.145382236097941,
0.159841449725047,0.163420463120145,0.165251746466431,0.167163469554063,
0.169379347146946,0.173172836430744,0.187843957056055,0.194634607030113,
0.232398675936394,0.257333668883158,0.268387954983155,0.270645518873576,
0.271898594097376,0.272970084500289,0.274321831658835,0.276453659046085,
0.287275067141506,0.291986924343857,0.292255738542014,0.299089676090735,
0.344016679468041,0.361673377650787,0.37247226116102,0.375775572990988,
0.37786076271535,0.379796649878384,0.38230890782771,0.386505067983572,0.416445511501366,
0.457610276871152,0.472691013384552,0.480712489556112,0.482755284556124,
0.483961048244808,0.485040368096117,0.486443047697802,0.488794591398675,
0.503847725139858,0.50417963064025,0.508484169232661,0.556501547347434,
0.580216269568659,0.586024222722498,0.588623458877811,0.590566149166089,
0.592384616724773,0.594895671029282,0.601345967063761,0.658910661578761,
0.681863226079149,0.692380929377794,0.69460594091003,0.69585197383282,0.696924280343102,
0.69828586238423,0.700449775966555,0.711789625384751,0.762836706960133,
0.791362040599131,0.797774181404231,0.800479162910151,0.802440117663382,
0.804233404117657,0.807102343025063,0.814011507442687,0.86678853168531,
0.892931787907377,0.904298204246441,0.906574054699768,0.907831176331421,
0.908902418230124,0.910249131646227,0.912866126801966,0.928828565608794,
0.929545427851628,0.973844302069392,1.00321075255303,1.00972273447401,1.01244458574824,
1.01440868736056,1.01619863283265,1.01904876395403,1.0258433586234,1.08004718552776,
1.10520899712734,1.11632331638331,1.11858464568805,1.11983864887484,1.120910222607,
1.12226116799733,1.12489765476065,1.14132677815376,1.19190998478661,1.20961968338314,
1.22044219744945,1.22374835298558,1.22583432822735,1.22777024940487,1.23028156702776,
1.23447399618861,1.25952994513294),.UNSPECIFIED.);
#1872=B_SPLINE_CURVE_WITH_KNOTS('',3,(#180249,#180250,#180251,#180252,#180253,
#180254,#180255,#180256,#180257,#180258,#180259,#180260,#180261,#180262,
#180263,#180264,#180265,#180266,#180267,#180268,#180269,#180270,#180271,
#180272,#180273,#180274,#180275,#180276,#180277,#180278,#180279,#180280,
#180281,#180282,#180283,#180284,#180285,#180286,#180287,#180288,#180289,
#180290,#180291,#180292,#180293,#180294,#180295,#180296,#180297,#180298,
#180299,#180300,#180301,#180302,#180303,#180304,#180305,#180306,#180307,
#180308,#180309,#180310,#180311,#180312,#180313,#180314,#180315,#180316,
#180317,#180318,#180319,#180320,#180321,#180322,#180323,#180324,#180325,
#180326,#180327,#180328,#180329,#180330,#180331,#180332,#180333,#180334,
#180335,#180336,#180337,#180338,#180339,#180340,#180341,#180342,#180343,
#180344,#180345,#180346,#180347,#180348,#180349,#180350,#180351,#180352,
#180353,#180354,#180355,#180356,#180357,#180358,#180359,#180360,#180361,
#180362,#180363,#180364,#180365,#180366,#180367,#180368,#180369,#180370,
#180371,#180372,#180373,#180374,#180375,#180376,#180377,#180378,#180379,
#180380,#180381,#180382,#180383,#180384,#180385,#180386,#180387,#180388,
#180389,#180390,#180391,#180392,#180393,#180394,#180395,#180396,#180397,
#180398,#180399,#180400,#180401,#180402,#180403,#180404,#180405,#180406,
#180407,#180408,#180409,#180410,#180411,#180412,#180413,#180414,#180415,
#180416,#180417,#180418,#180419,#180420,#180421,#180422,#180423,#180424,
#180425,#180426,#180427,#180428,#180429,#180430,#180431,#180432,#180433,
#180434,#180435,#180436,#180437,#180438,#180439,#180440,#180441,#180442,
#180443,#180444,#180445,#180446,#180447,#180448,#180449,#180450,#180451,
#180452,#180453,#180454,#180455,#180456,#180457,#180458,#180459,#180460,
#180461,#180462,#180463,#180464,#180465,#180466),.UNSPECIFIED.,.F.,.F.,
(4,2,2,2,2,2,2,2,2,2,2,2,2,2,2,2,2,2,2,2,2,2,2,2,2,2,2,2,2,2,2,2,2,2,2,
2,2,2,2,2,2,2,2,2,2,2,2,2,2,2,2,2,2,2,2,2,2,2,2,2,2,2,2,2,2,2,2,2,2,2,2,
2,2,2,2,2,2,2,2,2,2,2,2,2,2,2,2,2,2,2,2,2,2,2,2,2,2,2,2,2,2,2,2,2,2,2,2,
2,4),(1.40864677202052,1.42717364576226,1.46609541676906,1.47423845005591,
1.49151516819806,1.49418410944191,1.49554213256243,1.49661437793364,1.49786349370049,
1.50010182030058,1.51082885999856,1.53453385511464,1.56191062557594,1.59384737618265,
1.59808754277584,1.60061307280469,1.60255156194732,1.60463207368134,1.60791211342398,
1.61849509322632,1.6356638427404,1.68140178055422,1.68818809443002,1.70362499740722,
1.70599281398186,1.70740047378882,1.70848077396767,1.7096844891459,1.71171695329105,
1.71961256367361,1.73434144998214,1.76337580102843,1.80576310256087,1.81005680894429,
1.81259791662672,1.81453894986154,1.81661304119256,1.8198637714802,1.83018809678135,
1.84678009577227,1.8796966328426,1.8957088568118,1.89936901383237,1.91556025607603,
1.91818768760102,1.91953682008136,1.92060843647354,1.92186420908351,1.92413306833315,
1.93537222914556,1.96101030602208,2.01449202780544,2.02134631995769,2.0242066152825,
2.02599861757039,2.02796149101847,2.03067521466761,2.03713701056287,2.09109131045908,
2.12733130069677,2.13018646890341,2.13156373324646,2.13263766183573,2.13387345146592,
2.13605083075925,2.14583496536358,2.19473680294313,2.22986226626357,2.23415147433881,
2.23669122124905,2.2386319653576,2.24070647594637,2.24395938560466,2.25430350273394,
2.2709395883316,2.30389189654495,2.32204987328687,2.33956664036618,2.34224414499969,
2.34360397074656,2.34467632491935,2.34592406023346,2.34815617422359,2.35878323367491,
2.38212425015349,2.43905942078557,2.44557853004871,2.44810086625834,2.44992251969286,
2.45182509696711,2.4543389563836,2.45711929023671,2.47422092648888,2.50981441549534,
2.54858920483338,2.55333924153494,2.55508500962317,2.55611148224048,2.55720336957248,
2.55871061120539,2.56227466057451,2.59910852854178,2.64882446399773,2.65698836256091,
2.66005999003248,2.66189152253071,2.66373571134253,2.66602783958275,2.66809243247618),
 .UNSPECIFIED.);
#1873=B_SPLINE_CURVE_WITH_KNOTS('',3,(#180467,#180468,#180469,#180470,#180471,
#180472,#180473,#180474,#180475,#180476),.UNSPECIFIED.,.F.,.F.,(4,2,2,2,
4),(0.000823833555207768,0.00366228394810211,0.00932751687306586,0.0366377460792521,
0.0751066538684062),.UNSPECIFIED.);
#1874=B_SPLINE_CURVE_WITH_KNOTS('',3,(#180482,#180483,#180484,#180485,#180486,
#180487),.UNSPECIFIED.,.F.,.F.,(4,2,4),(2.59315592077889,2.60891629482103,
2.66742166566177),.UNSPECIFIED.);
#1875=B_SPLINE_CURVE_WITH_KNOTS('',3,(#180488,#180489,#180490,#180491,#180492,
#180493,#180494,#180495,#180496,#180497),.UNSPECIFIED.,.F.,.F.,(4,1,1,1,
1,1,1,4),(152.455231354966,152.821976844167,153.820813294129,154.819649744091,
155.818486194052,156.817322644014,157.816159093976,158.388969095546),
 .UNSPECIFIED.);
#1876=B_SPLINE_CURVE_WITH_KNOTS('',3,(#180498,#180499,#180500,#180501,#180502,
#180503,#180504,#180505,#180506,#180507,#180508,#180509,#180510,#180511,
#180512,#180513,#180514,#180515,#180516,#180517,#180518,#180519,#180520,
#180521,#180522,#180523,#180524,#180525,#180526,#180527,#180528,#180529,
#180530,#180531,#180532,#180533,#180534,#180535,#180536,#180537,#180538,
#180539,#180540,#180541,#180542,#180543,#180544,#180545,#180546,#180547,
#180548,#180549,#180550,#180551,#180552,#180553,#180554,#180555,#180556,
#180557,#180558,#180559,#180560,#180561,#180562,#180563,#180564,#180565,
#180566,#180567,#180568,#180569,#180570,#180571,#180572,#180573,#180574,
#180575,#180576,#180577,#180578,#180579,#180580,#180581,#180582,#180583,
#180584,#180585,#180586,#180587,#180588,#180589,#180590,#180591,#180592,
#180593,#180594,#180595,#180596,#180597,#180598,#180599,#180600,#180601,
#180602,#180603,#180604,#180605,#180606,#180607,#180608,#180609,#180610,
#180611,#180612,#180613,#180614,#180615,#180616,#180617,#180618,#180619,
#180620,#180621,#180622,#180623,#180624,#180625,#180626,#180627,#180628,
#180629,#180630,#180631,#180632,#180633,#180634,#180635,#180636,#180637,
#180638,#180639,#180640,#180641,#180642,#180643,#180644,#180645,#180646,
#180647,#180648,#180649,#180650,#180651,#180652,#180653,#180654,#180655,
#180656,#180657,#180658,#180659,#180660,#180661,#180662,#180663,#180664,
#180665,#180666,#180667,#180668,#180669,#180670,#180671,#180672,#180673,
#180674,#180675,#180676,#180677,#180678,#180679,#180680,#180681,#180682,
#180683,#180684,#180685,#180686,#180687,#180688,#180689,#180690,#180691,
#180692,#180693,#180694,#180695,#180696,#180697,#180698,#180699,#180700,
#180701,#180702,#180703,#180704,#180705,#180706,#180707,#180708,#180709,
#180710,#180711,#180712,#180713,#180714,#180715,#180716,#180717,#180718,
#180719,#180720,#180721,#180722,#180723,#180724,#180725,#180726,#180727,
#180728,#180729,#180730,#180731,#180732,#180733,#180734,#180735,#180736,
#180737,#180738,#180739,#180740,#180741,#180742,#180743,#180744,#180745),
 .UNSPECIFIED.,.F.,.F.,(4,2,2,2,2,2,2,2,2,2,2,2,2,2,2,2,2,2,2,2,2,2,2,2,
2,2,2,2,2,2,2,2,2,2,2,2,2,2,2,2,2,2,2,2,2,2,2,2,2,2,2,2,2,2,2,2,2,2,2,2,
2,2,2,2,2,2,2,2,2,2,2,2,2,2,2,2,2,2,2,2,2,2,2,2,2,2,2,2,2,2,2,2,2,2,2,2,
2,2,2,2,2,2,2,2,2,2,2,2,2,2,2,2,2,2,2,2,2,2,2,2,2,2,2,4),(0.0751066538684062,
0.0853464370458629,0.0970415719080759,0.0993358324161196,0.100596927831639,
0.101667827669287,0.103009388096851,0.105107785673461,0.115413356626747,
0.12067329748708,0.139468793162179,0.181309803440704,0.199977034375344,
0.202818257513735,0.205275670488441,0.207196708670981,0.208991016502369,
0.211865349820437,0.218790631706484,0.271285788687736,0.297629150870201,
0.309046253200314,0.311325043344881,0.312582827521975,0.313654051970842,
0.315000003570262,0.31761334854299,0.333490389110287,0.339268429871492,
0.378729182437409,0.407975659719928,0.414473668465978,0.417193258632019,
0.419157015533481,0.420947527455091,0.423800462764248,0.43061146404938,
0.484633539818862,0.509922005727839,0.521069529966652,0.523332882455269,
0.52458736213142,0.525658949069601,0.527009408273084,0.529136584894448,
0.539880483893609,0.545950872384997,0.549568907402696,0.595500673643667,
0.613961068927827,0.625110025414995,0.628451652918744,0.630545550707453,
0.632478962426192,0.634973176772787,0.639106945842207,0.666582324745711,
0.708929438223251,0.725014649531097,0.733392079130199,0.735464646410787,
0.736677168609629,0.737755144674835,0.739146485178004,0.741458868591958,
0.755618914432618,0.756947693765561,0.775377036237943,0.77771377382717,
0.810507456247192,0.83315022931624,0.838815680743529,0.841389321434246,
0.843328330608518,0.84515466292416,0.847694641618562,0.854322106688857,
0.910315161187398,0.93429138016885,0.945091386749922,0.947334196497143,
0.94858429027601,0.94965643833323,0.951013128343307,0.953160447902102,0.964222443799658,
1.01536897095973,1.0440936697049,1.05053028629531,1.05323977540908,1.05520188675337,
1.05699477868204,1.0598599266731,1.06674360217525,1.11988990105854,1.14579021437507,
1.15709595355743,1.15936870112171,1.16062532512125,1.16169688147637,1.16304493029893,
1.16566728427923,1.18171529530774,1.18582749280021,1.2015194330128,1.23440851705753,
1.25719722284593,1.26288266808008,1.26546015801674,1.26739994702939,1.26922545978457,
1.27176181064671,1.27836519705283,1.33460492043245,1.35355839492103,1.36856131134596,
1.37091144978739,1.37231399672715,1.37339364470637,1.3746002647154,1.37664556743915,
1.38469044903661,1.39983134679781,1.4087239097703),.UNSPECIFIED.);
#1877=B_SPLINE_CURVE_WITH_KNOTS('',3,(#180750,#180751,#180752,#180753,#180754,
#180755,#180756,#180757,#180758,#180759,#180760,#180761,#180762,#180763,
#180764,#180765,#180766,#180767,#180768,#180769,#180770,#180771,#180772,
#180773,#180774,#180775,#180776,#180777,#180778,#180779,#180780,#180781,
#180782,#180783,#180784,#180785,#180786,#180787,#180788,#180789,#180790,
#180791,#180792,#180793,#180794,#180795,#180796,#180797,#180798,#180799,
#180800,#180801,#180802,#180803,#180804,#180805,#180806,#180807,#180808,
#180809,#180810,#180811,#180812,#180813,#180814,#180815,#180816,#180817,
#180818,#180819,#180820,#180821,#180822,#180823,#180824,#180825,#180826,
#180827,#180828,#180829,#180830,#180831,#180832,#180833,#180834,#180835,
#180836,#180837,#180838,#180839,#180840,#180841,#180842,#180843,#180844,
#180845,#180846,#180847,#180848,#180849,#180850,#180851,#180852,#180853,
#180854,#180855,#180856,#180857,#180858,#180859,#180860,#180861,#180862,
#180863,#180864,#180865,#180866,#180867,#180868,#180869,#180870,#180871,
#180872,#180873,#180874,#180875,#180876,#180877,#180878,#180879,#180880,
#180881,#180882,#180883,#180884,#180885,#180886,#180887,#180888,#180889,
#180890,#180891,#180892,#180893,#180894,#180895,#180896,#180897,#180898,
#180899,#180900,#180901,#180902,#180903,#180904,#180905,#180906,#180907,
#180908,#180909,#180910,#180911,#180912,#180913,#180914,#180915,#180916,
#180917,#180918,#180919,#180920,#180921,#180922,#180923,#180924,#180925,
#180926,#180927,#180928,#180929,#180930,#180931,#180932,#180933,#180934,
#180935,#180936,#180937,#180938,#180939,#180940,#180941,#180942,#180943,
#180944,#180945,#180946,#180947,#180948,#180949,#180950,#180951,#180952,
#180953,#180954,#180955,#180956,#180957,#180958,#180959,#180960,#180961,
#180962,#180963,#180964,#180965,#180966,#180967,#180968,#180969,#180970,
#180971,#180972,#180973,#180974,#180975,#180976,#180977,#180978,#180979,
#180980,#180981,#180982,#180983),.UNSPECIFIED.,.F.,.F.,(4,2,2,2,2,2,2,2,
2,2,2,2,2,2,2,2,2,2,2,2,2,2,2,2,2,2,2,2,2,2,2,2,2,2,2,2,2,2,2,2,2,2,2,2,
2,2,2,2,2,2,2,2,2,2,2,2,2,2,2,2,2,2,2,2,2,2,2,2,2,2,2,2,2,2,2,2,2,2,2,2,
2,2,2,2,2,2,2,2,2,2,2,2,2,2,2,2,2,2,2,2,2,2,2,2,2,2,2,2,2,2,2,2,2,2,2,2,
4),(1.2596092854299,1.26784055751155,1.29070305347183,1.30119586103389,
1.30341928457475,1.30466495418703,1.3057372358087,1.30709916505989,1.30978755131927,
1.32763515166132,1.3337320471683,1.3757426351308,1.40292854294941,1.40705404625465,
1.40954560719511,1.41147833514597,1.413572861717,1.41691845641326,1.42810816206235,
1.44666703713446,1.49069768567924,1.49656848995899,1.51244824762357,1.515061588296,
1.51640744975573,1.51747862294526,1.51873640719983,1.52101504483251,1.53242879554278,
1.55875570591604,1.61123417420874,1.61816334580788,1.62103576852764,1.62282983345686,
1.62479052418754,1.62749309455207,1.63388986676,1.68178289775531,1.72137472810358,
1.72610769765945,1.72785089466736,1.72887687739298,1.7299690440267,1.73147806846267,
1.73505280596006,1.77424547541152,1.82298126420698,1.83011231019706,1.83301822396599,
1.83481837115166,1.8367739495846,1.83944819181053,1.84567960840533,1.87271680925558,
1.91343179187051,1.9361424106261,1.93899620386144,1.94037302386442,1.94144670813122,
1.94268232985773,1.94485968541373,1.95464821425903,2.00353413482948,2.03864072814747,
2.04293542352402,2.04547648503994,2.04741711898868,2.04949043046021,2.05273920036304,
2.06305106396055,2.07961707413574,2.11250732988003,2.12706654699959,2.1323852310817,
2.14842387306158,2.15104513512959,2.15239273817488,2.15346400914608,2.15472038860364,
2.15699287334563,2.16830152576631,2.19421530896038,2.24727738471828,2.2541619656418,
2.25702684114788,2.25881937754806,2.26078095698944,2.26348944196519,2.26992238015805,
2.29862621005349,2.34984861188788,2.36088133259416,2.36302657483499,2.36438248748561,
2.36545437861352,2.36670458817691,2.36894865199325,2.37977521518805,2.4038504481036,
2.45963405600161,2.46627495554774,2.46881672542427,2.47064329078775,2.47251929302347,
2.47500313974899,2.47774077498614,2.48229128053979,2.49161863124835,2.54225918008863,
2.57203620196739,2.57495057375471,2.57633918699828,2.57741401028942,2.57864192378382,
2.58078442024775,2.59007760248922,2.59315592077889),.UNSPECIFIED.);
#1878=B_SPLINE_CURVE_WITH_KNOTS('',3,(#180985,#180986,#180987,#180988,#180989,
#180990,#180991,#180992,#180993,#180994,#180995,#180996,#180997,#180998,
#180999,#181000,#181001,#181002,#181003,#181004,#181005,#181006,#181007,
#181008,#181009,#181010,#181011,#181012,#181013,#181014,#181015,#181016,
#181017,#181018,#181019,#181020,#181021,#181022,#181023,#181024,#181025,
#181026,#181027,#181028,#181029,#181030,#181031,#181032,#181033,#181034,
#181035,#181036,#181037,#181038,#181039,#181040,#181041,#181042,#181043,
#181044,#181045,#181046,#181047,#181048,#181049,#181050,#181051,#181052,
#181053,#181054,#181055,#181056,#181057,#181058,#181059,#181060,#181061,
#181062,#181063,#181064,#181065,#181066,#181067,#181068,#181069,#181070,
#181071,#181072,#181073,#181074,#181075,#181076,#181077,#181078,#181079,
#181080,#181081,#181082,#181083,#181084,#181085,#181086,#181087,#181088,
#181089,#181090,#181091,#181092,#181093,#181094,#181095,#181096,#181097,
#181098,#181099,#181100,#181101,#181102,#181103,#181104,#181105,#181106,
#181107,#181108,#181109,#181110,#181111,#181112,#181113,#181114,#181115,
#181116,#181117,#181118,#181119,#181120,#181121,#181122,#181123,#181124,
#181125,#181126,#181127,#181128,#181129,#181130,#181131,#181132,#181133,
#181134,#181135,#181136,#181137,#181138,#181139,#181140,#181141,#181142,
#181143,#181144,#181145,#181146,#181147,#181148,#181149,#181150,#181151,
#181152,#181153,#181154,#181155,#181156,#181157,#181158,#181159,#181160,
#181161,#181162,#181163,#181164,#181165,#181166,#181167,#181168,#181169,
#181170,#181171,#181172,#181173,#181174,#181175,#181176,#181177,#181178,
#181179,#181180,#181181,#181182,#181183,#181184,#181185,#181186,#181187,
#181188,#181189,#181190,#181191,#181192,#181193,#181194,#181195,#181196,
#181197,#181198,#181199,#181200,#181201,#181202,#181203,#181204,#181205,
#181206,#181207,#181208,#181209,#181210),.UNSPECIFIED.,.F.,.F.,(4,2,2,2,
2,2,2,2,2,2,2,2,2,2,2,2,2,2,2,2,2,2,2,2,2,2,2,2,2,2,2,2,2,2,2,2,2,2,2,2,
2,2,2,2,2,2,2,2,2,2,2,2,2,2,2,2,2,2,2,2,2,2,2,2,2,2,2,2,2,2,2,2,2,2,2,2,
2,2,2,2,2,2,2,2,2,2,2,2,2,2,2,2,2,2,2,2,2,2,2,2,2,2,2,2,2,2,2,2,2,2,2,2,
4),(1.4087239097703,1.43953310653064,1.4707906634425,1.47501726132828,1.47753894204538,
1.47947694358548,1.48155935196071,1.48484750803127,1.49550157222155,1.51282980903747,
1.55311717757715,1.58011104335949,1.58301346000418,1.58440002326499,1.58547494306089,
1.58670485223124,1.58885526017928,1.59825165920333,1.64749090277013,1.68271042221743,
1.68700767412,1.68954985110794,1.69149110854773,1.69356486489835,1.69681387046829,
1.7071226019063,1.72367991756045,1.75656825147938,1.77012258685533,1.77743785290147,
1.78179523708985,1.79296115305944,1.7951149407989,1.79647362262413,1.79754595605584,
1.79879467912652,1.80103106831506,1.81172554047372,1.83531077426319,1.89186564640622,
1.89843106897118,1.90096124141165,1.90278503575134,1.90472552121993,1.90730824366264,
1.91302294624607,1.93603367005409,1.96909147498953,1.99034868695485,2.0046763164207,
2.00699835131973,2.00839255421045,2.00947093981632,2.01068191140972,2.01274734029082,
2.02103661059078,2.03686696109282,2.07904331309759,2.10698563685207,2.1111315541083,
2.11362941753169,2.1155634687185,2.11765587684943,2.12099040864645,2.13207178847149,
2.15037766535872,2.19869324226627,2.21644768555504,2.2191335159248,2.22049512370589,
2.22156762814829,2.22281410102886,2.22504040537006,2.23557399195102,2.25857773083565,
2.31603906537968,2.32250093672487,2.32501419885246,2.32683348917125,2.32877633456139,
2.33137452002162,2.33717482919308,2.36083020557867,2.39173684265513,2.42827449457615,
2.43112334198816,2.4324992669988,2.43357296085789,2.43478455334195,2.43688094777454,
2.43946832806807,2.44484972478038,2.46014569794909,2.50065627361534,2.53090695350227,
2.53511069881581,2.53762547072958,2.5395620976429,2.54164690306083,2.54494708699777,
2.55571316586618,2.57329622979357,2.61947477386722,2.62780655258086,2.64081202452361,
2.64306759883811,2.64445699598947,2.64553204210694,2.64654087036144,2.64775405385555,
2.64954048691474,2.65527579181324,2.66794445739932),.UNSPECIFIED.);
#1879=B_SPLINE_CURVE_WITH_KNOTS('',3,(#181211,#181212,#181213,#181214,#181215,
#181216,#181217,#181218,#181219,#181220,#181221,#181222,#181223),
 .UNSPECIFIED.,.F.,.F.,(4,3,3,3,4),(-161.271232361061,-161.169466150914,
-161.067655442619,-160.965693965034,-160.920671713183),.UNSPECIFIED.);
#1880=B_SPLINE_CURVE_WITH_KNOTS('',3,(#181229,#181230,#181231,#181232,#181233,
#181234,#181235,#181236,#181237,#181238,#181239,#181240,#181241),
 .UNSPECIFIED.,.F.,.F.,(4,3,3,3,4),(170.955339710339,171.057208844779,171.158971097412,
171.260660135508,171.305836564222),.UNSPECIFIED.);
#1881=B_SPLINE_CURVE_WITH_KNOTS('',3,(#181242,#181243,#181244,#181245,#181246,
#181247,#181248,#181249,#181250,#181251,#181252,#181253,#181254,#181255,
#181256,#181257,#181258,#181259,#181260,#181261,#181262,#181263,#181264,
#181265,#181266,#181267,#181268,#181269,#181270,#181271,#181272,#181273,
#181274,#181275,#181276,#181277,#181278,#181279,#181280,#181281,#181282,
#181283,#181284,#181285,#181286,#181287,#181288,#181289,#181290,#181291,
#181292,#181293,#181294,#181295,#181296,#181297,#181298,#181299,#181300,
#181301,#181302,#181303,#181304,#181305,#181306,#181307,#181308,#181309,
#181310,#181311,#181312,#181313,#181314,#181315,#181316,#181317,#181318,
#181319,#181320,#181321,#181322,#181323,#181324,#181325,#181326,#181327,
#181328,#181329,#181330,#181331,#181332,#181333,#181334,#181335,#181336,
#181337,#181338,#181339,#181340,#181341,#181342,#181343,#181344,#181345,
#181346,#181347,#181348,#181349,#181350,#181351,#181352,#181353,#181354,
#181355,#181356,#181357,#181358,#181359,#181360,#181361,#181362,#181363,
#181364,#181365,#181366,#181367,#181368,#181369,#181370,#181371,#181372,
#181373,#181374,#181375,#181376,#181377,#181378,#181379,#181380,#181381,
#181382,#181383,#181384,#181385,#181386,#181387,#181388,#181389,#181390,
#181391,#181392,#181393,#181394,#181395,#181396,#181397,#181398,#181399,
#181400,#181401,#181402,#181403,#181404,#181405,#181406,#181407,#181408,
#181409,#181410,#181411,#181412,#181413,#181414,#181415,#181416,#181417,
#181418,#181419,#181420,#181421,#181422,#181423,#181424,#181425,#181426,
#181427,#181428,#181429,#181430,#181431,#181432,#181433,#181434,#181435,
#181436,#181437,#181438,#181439,#181440,#181441,#181442,#181443,#181444,
#181445,#181446,#181447,#181448,#181449,#181450,#181451,#181452,#181453,
#181454,#181455,#181456,#181457,#181458,#181459,#181460,#181461,#181462,
#181463),.UNSPECIFIED.,.F.,.F.,(4,2,2,2,2,2,2,2,2,2,2,2,2,2,2,2,2,2,2,2,
2,2,2,2,2,2,2,2,2,2,2,2,2,2,2,2,2,2,2,2,2,2,2,2,2,2,2,2,2,2,2,2,2,2,2,2,
2,2,2,2,2,2,2,2,2,2,2,2,2,2,2,2,2,2,2,2,2,2,2,2,2,2,2,2,2,2,2,2,2,2,2,2,
2,2,2,2,2,2,2,2,2,2,2,2,2,2,2,2,2,2,4),(0.000655553105071722,0.0215327022503399,
0.0285521141267371,0.0303960812882683,0.0316335720171466,0.0326484433143034,
0.0337175298956809,0.0350634467520839,0.0377856129526834,0.0559582137427058,
0.0616381071511329,0.0739377920509654,0.0845184420705206,0.106384465137635,
0.122977060357035,0.133286033526241,0.136520200021145,0.138580642265221,
0.140506650842285,0.143024722911443,0.147271547765017,0.192337554227069,
0.220917548979898,0.234450971820541,0.241868990982089,0.243841387940844,
0.244851109631307,0.245918148677256,0.247244764407309,0.249294095405719,
0.258883090837928,0.318505477136906,0.335297061926008,0.345718734013405,
0.348984761231629,0.351065048444871,0.353009420737682,0.35555141705698,
0.359839125091224,0.394233009182222,0.44343552787257,0.453287201291696,
0.455474777349829,0.456715751415926,0.457792016017413,0.459170679611106,
0.462028585192884,0.484806459207241,0.527329152876518,0.545904429014042,
0.557102195141594,0.560449714400349,0.562545379780961,0.564479121375145,
0.566971944221895,0.571099464639318,0.598278064866925,0.640347506189968,
0.656908029981825,0.66544956728105,0.667534904237756,0.66875003530653,0.669826485917343,
0.671211219103108,0.673503612986742,0.68728756877378,0.698620809126769,
0.737949711512445,0.764492303067573,0.770660366503347,0.773322007001096,
0.775273831587008,0.777074347835149,0.779989349136334,0.787184849384752,
0.833863017380337,0.856213770649654,0.870037647785498,0.875062775891369,
0.878645299588949,0.880154594737846,0.881246030472107,0.882271314704293,
0.884011288224965,0.888723642665489,0.929074950392337,0.977358991268938,
0.982966730790509,0.985529988135733,0.987467663862014,0.989297530270643,
0.991850143526969,0.998557329207836,1.05366061574855,1.07817670571631,1.08912119122043,
1.09137328851315,1.09262570504106,1.09369780575127,1.09505199526529,1.09779133641041,
1.1161497469021,1.16514969113898,1.18898303318183,1.19480675563528,1.19740896224039,
1.19935225338315,1.20117011145434,1.20367847276004,1.21011174277809,1.2596092854299),
 .UNSPECIFIED.);
#1882=B_SPLINE_CURVE_WITH_KNOTS('',3,(#181465,#181466,#181467,#181468,#181469,
#181470,#181471,#181472,#181473,#181474,#181475,#181476,#181477,#181478,
#181479,#181480,#181481,#181482,#181483,#181484,#181485,#181486,#181487,
#181488,#181489,#181490,#181491,#181492,#181493,#181494,#181495,#181496,
#181497,#181498,#181499,#181500,#181501,#181502,#181503,#181504,#181505,
#181506,#181507,#181508,#181509,#181510,#181511,#181512,#181513,#181514,
#181515,#181516,#181517,#181518,#181519,#181520,#181521,#181522,#181523,
#181524,#181525,#181526,#181527,#181528,#181529,#181530,#181531,#181532,
#181533,#181534,#181535,#181536,#181537,#181538,#181539,#181540,#181541,
#181542,#181543,#181544,#181545,#181546,#181547,#181548,#181549,#181550,
#181551,#181552,#181553,#181554,#181555,#181556,#181557,#181558,#181559,
#181560,#181561,#181562,#181563,#181564,#181565,#181566,#181567,#181568,
#181569,#181570,#181571,#181572,#181573,#181574,#181575,#181576,#181577,
#181578,#181579,#181580,#181581,#181582,#181583,#181584,#181585,#181586,
#181587,#181588,#181589,#181590,#181591,#181592,#181593,#181594,#181595,
#181596,#181597,#181598,#181599,#181600,#181601,#181602,#181603,#181604,
#181605,#181606,#181607,#181608,#181609,#181610,#181611,#181612,#181613,
#181614,#181615,#181616,#181617,#181618,#181619,#181620,#181621,#181622,
#181623,#181624,#181625,#181626,#181627,#181628,#181629,#181630,#181631,
#181632,#181633,#181634,#181635,#181636,#181637,#181638,#181639,#181640,
#181641,#181642,#181643,#181644,#181645),.UNSPECIFIED.,.F.,.F.,(4,3,3,3,
3,3,3,3,3,3,3,3,3,3,3,3,3,3,3,3,3,3,3,3,3,3,3,3,3,3,3,3,3,3,3,3,3,3,3,3,
3,3,3,3,3,3,3,3,3,3,3,3,3,3,3,3,3,3,3,3,4),(-167.203857019737,-167.089811057167,
-166.975344515757,-166.860315160037,-166.805687143633,-166.702287412998,
-166.599041100617,-166.495916074883,-166.392856430485,-166.289828137571,
-166.186797209444,-166.083659391335,-165.980465259865,-165.877088300924,
-165.806850693671,-165.703453680512,-165.600210065146,-165.497087692246,
-165.394030672044,-165.291004970728,-165.187976597605,-165.084841259846,
-164.981649570783,-164.878274965339,-164.808014243709,-164.70462213054,
-164.601383514262,-164.4982662645,-164.39521444117,-164.292194002951,-164.189170951718,
-164.08604098996,-163.982854715524,-163.879485527151,-163.809177793747,
-163.705782195438,-163.602540043866,-163.499419201028,-163.396363750916,
-163.293339657491,-163.190312927878,-163.087179277445,-162.983989302849,
-162.880616436887,-162.810341343786,-162.706946383752,-162.603704871948,
-162.500584667936,-162.39752985573,-162.294506398346,-162.191480301959,
-162.088347275963,-161.985157921851,-161.881785663032,-161.811504893824,
-161.709471729847,-161.607582180192,-161.505807287711,-161.404097849845,
-161.30240517996,-161.271232361061),.UNSPECIFIED.);
#1883=B_SPLINE_CURVE_WITH_KNOTS('',3,(#181646,#181647,#181648,#181649,#181650,
#181651,#181652,#181653,#181654,#181655,#181656,#181657,#181658),
 .UNSPECIFIED.,.F.,.F.,(4,3,3,3,4),(-167.553337655846,-167.448855737649,
-167.344457493798,-167.24011056783,-167.203857020092),.UNSPECIFIED.);
#1884=B_SPLINE_CURVE_WITH_KNOTS('',3,(#181664,#181665,#181666,#181667,#181668,
#181669,#181670,#181671,#181672,#181673),.UNSPECIFIED.,.F.,.F.,(4,3,3,4),
(7.5925217235916,7.70650211118153,7.82442142970536,7.9423407482292),
 .UNSPECIFIED.);
#1885=B_SPLINE_CURVE_WITH_KNOTS('',3,(#181675,#181676,#181677,#181678,#181679,
#181680,#181681,#181682,#181683,#181684,#181685,#181686,#181687,#181688,
#181689,#181690,#181691,#181692,#181693,#181694,#181695,#181696,#181697,
#181698,#181699,#181700,#181701,#181702,#181703,#181704,#181705,#181706,
#181707,#181708,#181709,#181710,#181711,#181712,#181713,#181714,#181715,
#181716,#181717,#181718,#181719,#181720,#181721,#181722,#181723,#181724,
#181725,#181726,#181727,#181728,#181729,#181730,#181731,#181732,#181733,
#181734,#181735,#181736,#181737,#181738,#181739,#181740,#181741,#181742,
#181743,#181744,#181745,#181746,#181747,#181748,#181749,#181750,#181751,
#181752,#181753,#181754,#181755,#181756,#181757,#181758,#181759,#181760,
#181761,#181762,#181763,#181764,#181765,#181766,#181767,#181768,#181769,
#181770,#181771,#181772,#181773,#181774,#181775,#181776,#181777,#181778,
#181779,#181780,#181781,#181782,#181783,#181784,#181785,#181786,#181787,
#181788,#181789,#181790,#181791,#181792,#181793,#181794,#181795,#181796,
#181797,#181798,#181799,#181800,#181801,#181802,#181803,#181804,#181805,
#181806,#181807,#181808,#181809,#181810,#181811,#181812,#181813,#181814,
#181815,#181816,#181817,#181818,#181819,#181820,#181821,#181822,#181823,
#181824,#181825,#181826,#181827,#181828,#181829,#181830,#181831,#181832,
#181833,#181834,#181835,#181836,#181837,#181838,#181839,#181840,#181841,
#181842,#181843),.UNSPECIFIED.,.F.,.F.,(4,3,3,3,3,3,3,3,3,3,3,3,3,3,3,3,
3,3,3,3,3,3,3,3,3,3,3,3,3,3,3,3,3,3,3,3,3,3,3,3,3,3,3,3,3,3,3,3,3,3,3,3,
3,3,3,3,4),(2.0087845179796,2.11210382153695,2.21526971314845,2.31831418782041,
2.42129345937132,2.52424167355639,2.62719293310599,2.73024899451789,2.83336205194679,
2.93665137518728,2.99650934988562,3.1000822938161,3.20350554280194,3.30681219802197,
3.41005626110442,3.51327148737703,3.6164915916683,3.71982072762223,3.82320766651892,
3.92677769686775,3.9953457998475,4.09860816546045,4.20171516905871,4.30469864795499,
4.40761543749361,4.51049977143286,4.61338583911071,4.71637840074725,4.81942682496833,
4.92265896654802,4.99418224980937,5.09760356589106,5.2008715269481,5.30401818826614,
5.40709944854822,5.51014930542212,5.61320171332599,5.71636073031363,5.81957593612843,
5.92297353214023,5.99301869977125,6.09643423322203,6.19969677808622,6.30283860095653,
6.40591538148351,6.50896112490232,6.61200979362756,6.71516567854847,6.81837808737288,
6.92177346211854,6.99185514973312,7.09670699527071,7.20139082935589,7.30591391683331,
7.41034217631691,7.5147117225697,7.59252172323623),.UNSPECIFIED.);
#1886=B_SPLINE_CURVE_WITH_KNOTS('',3,(#181847,#181848,#181849,#181850,#181851,
#181852,#181853,#181854,#181855,#181856,#181857,#181858,#181859,#181860,
#181861,#181862,#181863,#181864,#181865,#181866,#181867,#181868,#181869,
#181870,#181871,#181872,#181873,#181874,#181875,#181876,#181877,#181878,
#181879,#181880,#181881,#181882,#181883,#181884,#181885,#181886,#181887,
#181888,#181889,#181890,#181891,#181892,#181893,#181894,#181895,#181896,
#181897,#181898,#181899,#181900,#181901,#181902,#181903,#181904,#181905,
#181906,#181907,#181908,#181909,#181910,#181911,#181912,#181913,#181914,
#181915,#181916,#181917,#181918,#181919,#181920,#181921,#181922,#181923,
#181924,#181925,#181926,#181927,#181928,#181929,#181930,#181931,#181932,
#181933,#181934,#181935,#181936,#181937,#181938,#181939,#181940,#181941,
#181942,#181943,#181944,#181945,#181946,#181947,#181948,#181949,#181950,
#181951,#181952,#181953,#181954,#181955,#181956,#181957,#181958,#181959,
#181960,#181961,#181962,#181963,#181964),.UNSPECIFIED.,.F.,.F.,(4,3,3,3,
3,3,3,3,3,3,3,3,3,3,3,3,3,3,3,3,3,3,3,3,3,3,3,3,3,3,3,3,3,3,3,3,3,3,3,4),
(-3.8410390329882,-3.73547282260038,-3.63371534136024,-3.53202564994167,
-3.43036801697593,-3.32870675963968,-3.22694496840103,-3.12512265251928,
-3.02313914541121,-2.99650934988562,-2.89298805351485,-2.78961775740447,
-2.68636579627284,-2.58317747650149,-2.48001897640827,-2.37685651582112,
-2.27358608503736,-2.17025853571448,-2.06674838352885,-1.99767289992375,
-1.89536967835424,-1.79322051059792,-1.69118874726443,-1.58921969074132,
-1.48727797529671,-1.3853282756702,-1.28325622478001,-1.18112117613606,
-1.07878042700533,-0.998836449961875,-0.892562662128034,-0.78099232936203,
-0.675071864520977,-0.569250995903944,-0.463501983636266,-0.357797177553288,
-0.252079241114024,-0.146356223433945,-0.0405602493167351,0.),
 .UNSPECIFIED.);
#1887=B_SPLINE_CURVE_WITH_KNOTS('',3,(#181965,#181966,#181967,#181968,#181969,
#181970,#181971,#181972,#181973,#181974,#181975,#181976,#181977,#181978,
#181979,#181980,#181981,#181982,#181983,#181984,#181985,#181986,#181987,
#181988,#181989,#181990),.UNSPECIFIED.,.F.,.F.,(4,2,2,2,2,2,2,2,2,2,2,2,
4),(0.000655568072780243,0.0215326044780164,0.0285520611652364,0.0303960587346235,
0.0316335581114911,0.032648425183238,0.0337175017371922,0.0350633807412954,
0.0377853867802569,0.0559535320639813,0.0616384514068862,0.0739384345531311,
0.0747573385915169),.UNSPECIFIED.);
#1888=B_SPLINE_CURVE_WITH_KNOTS('',3,(#181996,#181997,#181998,#181999,#182000,
#182001,#182002,#182003,#182004,#182005,#182006,#182007,#182008,#182009,
#182010,#182011,#182012,#182013,#182014,#182015,#182016,#182017,#182018,
#182019),.UNSPECIFIED.,.F.,.F.,(4,2,2,2,2,2,2,2,2,2,2,4),(2.59366994486789,
2.61937244280716,2.62770429439083,2.64070987224822,2.64296546588963,2.64435487507994,
2.64542993062086,2.64643876778755,2.64765196207014,2.64943841110757,2.65517376483347,
2.66784253617411),.UNSPECIFIED.);
#1889=B_SPLINE_CURVE_WITH_KNOTS('',3,(#182020,#182021,#182022,#182023,#182024,
#182025,#182026,#182027,#182028,#182029,#182030,#182031,#182032,#182033,
#182034,#182035,#182036,#182037,#182038,#182039,#182040,#182041,#182042,
#182043,#182044,#182045,#182046,#182047,#182048,#182049,#182050,#182051,
#182052,#182053,#182054,#182055,#182056,#182057,#182058,#182059,#182060,
#182061,#182062,#182063,#182064,#182065,#182066,#182067,#182068,#182069,
#182070,#182071,#182072,#182073,#182074,#182075,#182076,#182077,#182078,
#182079,#182080,#182081,#182082,#182083,#182084,#182085,#182086,#182087,
#182088,#182089,#182090,#182091,#182092,#182093,#182094,#182095,#182096,
#182097,#182098,#182099,#182100,#182101,#182102,#182103,#182104,#182105,
#182106,#182107,#182108,#182109,#182110,#182111,#182112,#182113,#182114,
#182115,#182116,#182117,#182118,#182119,#182120,#182121,#182122,#182123,
#182124,#182125,#182126,#182127,#182128,#182129,#182130,#182131,#182132,
#182133,#182134,#182135,#182136,#182137,#182138,#182139,#182140,#182141,
#182142,#182143,#182144,#182145,#182146,#182147,#182148,#182149,#182150,
#182151,#182152,#182153,#182154,#182155,#182156,#182157,#182158,#182159,
#182160,#182161,#182162,#182163,#182164,#182165,#182166,#182167,#182168,
#182169,#182170,#182171,#182172,#182173,#182174,#182175,#182176,#182177,
#182178,#182179,#182180,#182181,#182182,#182183,#182184,#182185,#182186,
#182187,#182188,#182189,#182190,#182191,#182192,#182193,#182194,#182195,
#182196,#182197,#182198,#182199,#182200),.UNSPECIFIED.,.F.,.F.,(4,3,3,3,
3,3,3,3,3,3,3,3,3,3,3,3,3,3,3,3,3,3,3,3,3,3,3,3,3,3,3,3,3,3,3,3,3,3,3,3,
3,3,3,3,3,3,3,3,3,3,3,3,3,3,3,3,3,3,3,3,4),(7.9423407482292,7.99069159969499,
8.09409131510382,8.1973376121055,8.30046262230383,8.40352225107942,8.50655052830579,
8.6095814407028,8.71271924312554,8.81591335890946,8.91929030233818,8.98952804965687,
9.0929250599491,9.19616867235508,9.29929104216923,9.40234805920861,9.50537375729145,
9.60840212711332,9.71153746148904,9.81472914711778,9.91810374908263,9.98836449961874,
10.0917566194232,10.1949952424428,10.2981124990724,10.4011643293445,10.5041847745688,
10.6072078328613,10.7103378017146,10.813524083277,10.9168932787461,10.9872009495806,
11.0905965448759,11.1938386934009,11.2969595331577,11.40001498017,11.5030390704798,
11.6060657969671,11.7091994442799,11.8123894157543,11.9157622786263,11.9860373995425,
12.0894323592657,12.1926738707447,12.2957940744116,12.3988488862601,12.5018723432752,
12.6048984392812,12.708031464883,12.8112208185909,12.9145930769959,12.9848738495044,
13.0869196153942,13.1887917832796,13.2905669753687,13.3922809425427,13.4939693506563,
13.5957283288954,13.6975220044616,13.7994743438963,13.8757070301446),
 .UNSPECIFIED.);
#1890=B_SPLINE_CURVE_WITH_KNOTS('',3,(#182201,#182202,#182203,#182204,#182205,
#182206,#182207,#182208,#182209,#182210,#182211,#182212,#182213,#182214,
#182215,#182216,#182217,#182218,#182219,#182220,#182221,#182222,#182223,
#182224,#182225,#182226,#182227,#182228,#182229,#182230,#182231,#182232,
#182233,#182234,#182235,#182236,#182237,#182238,#182239,#182240,#182241,
#182242,#182243,#182244,#182245,#182246,#182247,#182248,#182249,#182250,
#182251,#182252,#182253,#182254,#182255,#182256,#182257,#182258,#182259,
#182260,#182261,#182262,#182263,#182264,#182265,#182266,#182267,#182268,
#182269,#182270,#182271,#182272,#182273,#182274,#182275,#182276,#182277,
#182278,#182279,#182280,#182281,#182282,#182283,#182284,#182285,#182286,
#182287,#182288,#182289,#182290,#182291,#182292,#182293,#182294,#182295,
#182296,#182297,#182298,#182299,#182300,#182301,#182302,#182303,#182304,
#182305,#182306,#182307,#182308,#182309,#182310,#182311,#182312,#182313,
#182314,#182315,#182316,#182317,#182318,#182319,#182320,#182321,#182322,
#182323,#182324,#182325,#182326,#182327,#182328,#182329,#182330,#182331,
#182332,#182333,#182334,#182335,#182336,#182337,#182338,#182339,#182340,
#182341,#182342,#182343,#182344,#182345,#182346,#182347,#182348,#182349,
#182350,#182351,#182352,#182353,#182354,#182355,#182356,#182357,#182358,
#182359,#182360,#182361,#182362,#182363,#182364,#182365,#182366,#182367,
#182368,#182369,#182370,#182371,#182372,#182373,#182374,#182375,#182376,
#182377,#182378,#182379,#182380,#182381,#182382,#182383,#182384,#182385,
#182386,#182387,#182388,#182389,#182390,#182391,#182392,#182393,#182394,
#182395,#182396,#182397,#182398,#182399,#182400,#182401,#182402,#182403,
#182404,#182405,#182406,#182407,#182408,#182409,#182410,#182411,#182412,
#182413,#182414,#182415,#182416,#182417,#182418,#182419,#182420,#182421,
#182422,#182423,#182424,#182425,#182426),.UNSPECIFIED.,.F.,.F.,(4,2,2,2,
2,2,2,2,2,2,2,2,2,2,2,2,2,2,2,2,2,2,2,2,2,2,2,2,2,2,2,2,2,2,2,2,2,2,2,2,
2,2,2,2,2,2,2,2,2,2,2,2,2,2,2,2,2,2,2,2,2,2,2,2,2,2,2,2,2,2,2,2,2,2,2,2,
2,2,2,2,2,2,2,2,2,2,2,2,2,2,2,2,2,2,2,2,2,2,2,2,2,2,2,2,2,2,2,2,2,2,2,2,
4),(0.0747573385915169,0.0845186660563088,0.106384825885023,0.122977264307818,
0.133286153510231,0.136520297104307,0.138580725314274,0.140506721079582,
0.14302477673237,0.147271574297925,0.192338068386794,0.220918198232181,
0.23445132046961,0.241869215344308,0.243841592621727,0.244851307008202,
0.245918344988499,0.247244964389105,0.249294304929312,0.258883412682225,
0.318505114363265,0.335297165839,0.345719059569437,0.348985119972811,0.351065419812425,
0.35300979800306,0.355551793623918,0.35983948206055,0.394231696268526,0.443432679699405,
0.453286801430609,0.455474553210324,0.456715570777116,0.457791834590142,
0.459170447891583,0.462028090662232,0.484795377877622,0.527329643639262,
0.545904467140845,0.557102035876837,0.56044953361568,0.562545193908041,
0.564478936499098,0.566971768575439,0.571099321372655,0.59827916816761,
0.640351409167709,0.656909155895798,0.665449741003629,0.667535000112857,
0.668750112633886,0.669826564784798,0.671211323074965,0.673503806328032,
0.687289664657288,0.69862343776508,0.737950307791625,0.764492433751154,
0.770660435514412,0.773322062769965,0.775273882640514,0.777074398031094,
0.779989405707813,0.787184959843073,0.833860461124851,0.856214196184002,
0.870037819475752,0.875062883147794,0.878645370113907,0.880154657585907,
0.881246091026226,0.882271376787971,0.88401135771577,0.888723760194312,
0.929076048762534,0.977359082455919,0.98296681558263,0.985530072725587,
0.98746774942837,0.989297617601982,0.991850234692957,0.998557439042445,
1.05366042498685,1.07817664904728,1.08912117123381,1.09137327239189,1.09262569060441,
1.09369779185165,1.09505198122705,1.09779132125902,1.11614969273561,1.16514965487027,
1.18898299316969,1.19480671436024,1.19740892035612,1.19935221102246,1.20117006862932,
1.20367842925972,1.21011169732687,1.26784057178093,1.29070305835673,1.30119586269071,
1.3034192852407,1.30466495423351,1.30573723528824,1.30709916372239,1.30978754800495,
1.32763511724923,1.33373204591263,1.37574265895549,1.40292854694586,1.40705404852227,
1.40817975905822),.UNSPECIFIED.);
#1891=B_SPLINE_CURVE_WITH_KNOTS('',3,(#182431,#182432,#182433,#182434,#182435,
#182436,#182437,#182438,#182439,#182440,#182441,#182442,#182443,#182444,
#182445,#182446,#182447,#182448,#182449,#182450,#182451,#182452,#182453,
#182454,#182455,#182456,#182457,#182458,#182459,#182460,#182461,#182462,
#182463,#182464,#182465,#182466,#182467,#182468,#182469,#182470,#182471,
#182472,#182473,#182474,#182475,#182476,#182477,#182478,#182479,#182480,
#182481,#182482,#182483,#182484,#182485,#182486,#182487,#182488,#182489,
#182490,#182491,#182492,#182493,#182494,#182495,#182496,#182497,#182498,
#182499,#182500,#182501,#182502,#182503,#182504,#182505,#182506,#182507,
#182508,#182509,#182510,#182511,#182512,#182513,#182514,#182515,#182516,
#182517,#182518,#182519,#182520,#182521,#182522,#182523,#182524,#182525,
#182526,#182527,#182528,#182529,#182530,#182531,#182532,#182533,#182534,
#182535,#182536,#182537,#182538,#182539,#182540,#182541,#182542,#182543,
#182544,#182545,#182546,#182547,#182548,#182549,#182550,#182551,#182552,
#182553,#182554,#182555,#182556,#182557,#182558,#182559,#182560,#182561,
#182562,#182563,#182564,#182565,#182566,#182567,#182568,#182569,#182570,
#182571,#182572,#182573,#182574,#182575,#182576,#182577,#182578,#182579,
#182580,#182581,#182582,#182583,#182584,#182585,#182586,#182587,#182588,
#182589,#182590,#182591,#182592,#182593,#182594,#182595,#182596,#182597,
#182598,#182599,#182600,#182601,#182602,#182603,#182604,#182605,#182606,
#182607,#182608,#182609,#182610,#182611,#182612,#182613,#182614,#182615,
#182616,#182617,#182618,#182619,#182620,#182621,#182622,#182623,#182624,
#182625,#182626,#182627,#182628,#182629,#182630,#182631,#182632,#182633,
#182634,#182635,#182636,#182637,#182638,#182639,#182640,#182641,#182642,
#182643,#182644,#182645,#182646,#182647,#182648,#182649,#182650,#182651,
#182652,#182653,#182654,#182655,#182656,#182657,#182658,#182659,#182660,
#182661,#182662,#182663,#182664,#182665,#182666,#182667,#182668,#182669,
#182670),.UNSPECIFIED.,.F.,.F.,(4,2,2,2,2,2,2,2,2,2,2,2,2,2,2,2,2,2,2,2,
2,2,2,2,2,2,2,2,2,2,2,2,2,2,2,2,2,2,2,2,2,2,2,2,2,2,2,2,2,2,2,2,2,2,2,2,
2,2,2,2,2,2,2,2,2,2,2,2,2,2,2,2,2,2,2,2,2,2,2,2,2,2,2,2,2,2,2,2,2,2,2,2,
2,2,2,2,2,2,2,2,2,2,2,2,2,2,2,2,2,2,2,2,2,2,2,2,2,2,2,4),(1.26001551649135,
1.26284451446193,1.26542193188058,1.26736166623112,1.26918712748262,1.27172340669052,
1.27832660600844,1.33456473152628,1.35351766662686,1.3685201584845,1.37087023057504,
1.3722727379463,1.37335235548607,1.37455894150873,1.37660418670428,1.38464884310749,
1.39978931893419,1.43948999071047,1.47074661031438,1.4749730877135,1.47749469695244,
1.47943264379949,1.48151499364467,1.48480305780564,1.49545682878334,1.51278459355559,
1.55307079622017,1.58006388566935,1.58296622023713,1.58435274436055,1.58542763385194,
1.58665750840069,1.5888078559456,1.59820399318063,1.64744184496253,1.68266035164975,
1.6869574819605,1.68949958715262,1.69144078984891,1.69351448780033,1.69676340204889,
1.70707184529562,1.72362869984322,1.75651610810682,1.77007085800938,1.77738388897131,
1.78171825412594,1.7929054640263,1.79506051127956,1.79641955692446,1.79749189118573,
1.7987402867533,1.80097527400743,1.81164770871794,1.83515299066214,1.89182920221108,
1.89838103212265,1.90090897907839,1.90273215532822,1.90467289611173,1.9072575226087,
1.91298289930623,1.93607392014222,1.97017197925383,1.99144317212453,2.00471566552533,
2.00698464570543,2.00836320108285,2.00943960284404,2.01065978181404,2.01276681091004,
2.02158118209909,2.03894711697881,2.088036472038,2.09416320705489,2.10833735473455,
2.11208659754359,2.11429251955556,2.11620533660696,2.11855166345124,2.12305607934971,
2.15614905299671,2.20248416037468,2.21664646325623,2.21895902652945,2.22035043524351,
2.22142844140827,2.22264098294256,2.22471353626541,2.23309050027175,2.24917193431417,
2.29150102610325,2.3189604848539,2.323093695616,2.32558780982689,2.32752127384201,
2.32961535701129,2.33295755780525,2.34411090339026,2.36258384167035,2.39106624725118,
2.42818853789256,2.43102581077384,2.43239946690034,2.43347296076776,2.43468607022011,
2.43678917277774,2.43938677858613,2.44479786710206,2.46022018619701,2.50129051292669,
2.53082929599935,2.53501930970744,2.53753008116393,2.53946609955538,2.54155269066825,
2.54486091369059,2.55569990330907,2.57344886292543,2.59366994486789),
 .UNSPECIFIED.);
#1892=B_SPLINE_CURVE_WITH_KNOTS('',3,(#182672,#182673,#182674,#182675,#182676,
#182677,#182678,#182679,#182680,#182681,#182682,#182683,#182684,#182685,
#182686,#182687,#182688,#182689,#182690,#182691,#182692,#182693,#182694,
#182695,#182696,#182697,#182698,#182699,#182700,#182701,#182702,#182703,
#182704,#182705,#182706,#182707,#182708,#182709,#182710,#182711,#182712,
#182713,#182714,#182715,#182716,#182717,#182718,#182719,#182720,#182721,
#182722,#182723,#182724,#182725,#182726,#182727,#182728,#182729,#182730,
#182731,#182732,#182733,#182734,#182735,#182736,#182737,#182738,#182739,
#182740,#182741,#182742,#182743,#182744,#182745,#182746,#182747,#182748,
#182749,#182750,#182751,#182752,#182753,#182754,#182755,#182756,#182757,
#182758,#182759,#182760,#182761,#182762,#182763,#182764,#182765,#182766,
#182767,#182768,#182769,#182770,#182771,#182772,#182773,#182774,#182775,
#182776,#182777,#182778,#182779,#182780,#182781,#182782,#182783,#182784,
#182785,#182786,#182787,#182788,#182789,#182790,#182791,#182792,#182793,
#182794,#182795,#182796,#182797,#182798,#182799,#182800,#182801,#182802,
#182803,#182804,#182805,#182806,#182807,#182808,#182809,#182810,#182811,
#182812,#182813,#182814,#182815,#182816,#182817,#182818,#182819,#182820,
#182821,#182822,#182823,#182824,#182825,#182826,#182827,#182828,#182829,
#182830,#182831,#182832,#182833,#182834,#182835,#182836,#182837,#182838,
#182839,#182840,#182841,#182842,#182843,#182844,#182845,#182846,#182847,
#182848,#182849,#182850,#182851,#182852,#182853,#182854,#182855,#182856,
#182857,#182858,#182859,#182860,#182861,#182862,#182863,#182864,#182865,
#182866,#182867,#182868,#182869,#182870,#182871,#182872,#182873,#182874,
#182875,#182876,#182877,#182878,#182879,#182880,#182881),.UNSPECIFIED.,
 .F.,.F.,(4,2,2,2,2,2,2,2,2,2,2,2,2,2,2,2,2,2,2,2,2,2,2,2,2,2,2,2,2,2,2,
2,2,2,2,2,2,2,2,2,2,2,2,2,2,2,2,2,2,2,2,2,2,2,2,2,2,2,2,2,2,2,2,2,2,2,2,
2,2,2,2,2,2,2,2,2,2,2,2,2,2,2,2,2,2,2,2,2,2,2,2,2,2,2,2,2,2,2,2,2,2,2,2,
2,4),(1.40817975905822,1.40954560836466,1.41147833542434,1.4135728609852,
1.4169184539589,1.42810815255206,1.44666701369632,1.49069805568445,1.49656816369503,
1.51244823619313,1.51506158397542,1.51640744662406,1.51747861959037,1.5187364022801,
1.52101503315593,1.53242866855974,1.55875512241244,1.6112342419393,1.61816336723805,
1.62103578226236,1.62282984573923,1.62479053757248,1.62749311437592,1.63388992499525,
1.68180129896859,1.72137451500311,1.72610764874689,1.72785087070757,1.7288768583589,
1.72996902180997,1.73147802835959,1.7350526619759,1.77422308970196,1.82298257769147,
1.83011269461674,1.83301845230588,1.8348185704141,1.83677417067401,1.83944853898156,
1.8456806887981,1.87272384959603,1.91345069505711,1.93614315338508,1.93899650061353,
1.94037323279208,1.94144690848067,1.94268258799221,1.94486020732928,1.95465260962522,
2.00353525341999,2.03864078667319,2.04293546732949,2.0454765242656,2.04741715709159,
2.04949046966397,2.05273924608953,2.06305117074383,2.07961731710115,2.11250768493825,
2.12707675561372,2.13238317907733,2.1484237110747,2.1510450917114,2.15239272010833,
2.15346399253881,2.15472035205142,2.1569927456024,2.16829981653343,2.19420740046896,
2.2472783874386,2.25416228532456,2.25702704823045,2.25881956398771,2.26078116089898,
2.26348974349135,2.26992326198122,2.29863196938254,2.34984137610625,2.36088058032047,
2.36302622378498,2.36438225858115,2.365454158525,2.36670427744037,2.36894792669211,
2.37976766044285,2.40381758281657,2.45963978372236,2.46627671827603,2.46881786574529,
2.47064426615729,2.47252035325782,2.47500472435949,2.47774309062016,2.48229537649571,
2.49162780734091,2.54226190779155,2.57203626856797,2.57495063884984,2.57633925129826,
2.57741407393816,2.57864198664061,2.58078448159155,2.59007765512967,2.60891632565383,
2.66742169168651),.UNSPECIFIED.);
#1893=B_SPLINE_CURVE_WITH_KNOTS('',3,(#182882,#182883,#182884,#182885),
 .UNSPECIFIED.,.F.,.F.,(4,4),(-16.7565928334374,-16.4074096477818),
 .UNSPECIFIED.);
#1894=B_SPLINE_CURVE_WITH_KNOTS('',3,(#182891,#182892,#182893,#182894,#182895,
#182896,#182897,#182898,#182899,#182900,#182901,#182902,#182903,#182904,
#182905,#182906),.UNSPECIFIED.,.F.,.F.,(4,2,2,2,2,2,2,4),(2.59336419963794,
2.64851730992168,2.65667985504919,2.65975097327022,2.66158220209397,2.66342608512958,
2.66571783163649,2.66778208221742),.UNSPECIFIED.);
#1895=B_SPLINE_CURVE_WITH_KNOTS('',3,(#182907,#182908,#182909,#182910,#182911,
#182912,#182913,#182914,#182915,#182916,#182917,#182918,#182919,#182920,
#182921,#182922,#182923,#182924,#182925,#182926,#182927,#182928,#182929,
#182930,#182931,#182932,#182933,#182934,#182935,#182936,#182937,#182938,
#182939,#182940,#182941,#182942,#182943,#182944,#182945,#182946,#182947,
#182948,#182949,#182950,#182951,#182952,#182953,#182954,#182955,#182956,
#182957,#182958,#182959,#182960,#182961,#182962,#182963,#182964,#182965,
#182966,#182967,#182968,#182969,#182970,#182971,#182972,#182973,#182974,
#182975,#182976,#182977,#182978,#182979,#182980,#182981,#182982,#182983,
#182984,#182985,#182986,#182987,#182988,#182989,#182990,#182991,#182992,
#182993,#182994,#182995,#182996,#182997,#182998,#182999,#183000,#183001,
#183002,#183003,#183004,#183005,#183006,#183007,#183008,#183009,#183010,
#183011,#183012,#183013,#183014,#183015,#183016,#183017,#183018,#183019,
#183020,#183021,#183022,#183023,#183024,#183025,#183026,#183027,#183028,
#183029,#183030,#183031,#183032,#183033,#183034,#183035,#183036,#183037,
#183038,#183039,#183040,#183041,#183042,#183043,#183044,#183045,#183046,
#183047,#183048,#183049,#183050,#183051,#183052,#183053,#183054,#183055,
#183056,#183057,#183058,#183059,#183060,#183061,#183062,#183063,#183064,
#183065,#183066,#183067,#183068,#183069,#183070,#183071,#183072,#183073,
#183074,#183075,#183076,#183077,#183078,#183079,#183080,#183081,#183082,
#183083,#183084,#183085,#183086,#183087,#183088,#183089,#183090,#183091,
#183092,#183093,#183094,#183095,#183096,#183097,#183098,#183099,#183100,
#183101,#183102,#183103,#183104,#183105,#183106,#183107,#183108,#183109,
#183110,#183111,#183112,#183113,#183114,#183115,#183116,#183117,#183118,
#183119,#183120,#183121,#183122,#183123,#183124,#183125,#183126,#183127,
#183128,#183129,#183130,#183131,#183132,#183133,#183134,#183135,#183136,
#183137,#183138,#183139,#183140,#183141,#183142,#183143,#183144,#183145,
#183146,#183147,#183148,#183149,#183150,#183151,#183152,#183153,#183154,
#183155,#183156),.UNSPECIFIED.,.F.,.F.,(4,2,2,2,2,2,2,2,2,2,2,2,2,2,2,2,
2,2,2,2,2,2,2,2,2,2,2,2,2,2,2,2,2,2,2,2,2,2,2,2,2,2,2,2,2,2,2,2,2,2,2,2,
2,2,2,2,2,2,2,2,2,2,2,2,2,2,2,2,2,2,2,2,2,2,2,2,2,2,2,2,2,2,2,2,2,2,2,2,
2,2,2,2,2,2,2,2,2,2,2,2,2,2,2,2,2,2,2,2,2,2,2,2,2,2,2,2,2,2,2,2,2,2,2,2,
4),(0.000823822472317207,0.00402591699170803,0.0105189260068452,0.0602232793173974,
0.0858540471813482,0.0970894386700358,0.0993576796542626,0.100613114722003,
0.10168444953284,0.103033229329788,0.105659981548195,0.121848831178235,
0.172512225735023,0.190330720635742,0.20120062365209,0.203653936590393,
0.20593359915671,0.205948682438116,0.205964392968151,0.20598077332524,0.205997870265091,
0.206015735165232,0.206034424666561,0.20605400146026,0.206074535004654,
0.206096102575133,0.206118790454896,0.206142695340538,0.206167925992387,
0.206194605303977,0.206222872714743,0.206252887251777,0.206284831231239,
0.206318914962662,0.206355382557691,0.208228529534964,0.210616080072911,
0.215085114556155,0.241811493627869,0.285244653545143,0.301115650922831,
0.309417858485812,0.311484081130193,0.312695075444056,0.313773183340093,
0.315166628301309,0.317486560700479,0.331786262924069,0.380028863003848,
0.40816513095325,0.414530534597715,0.417227561634384,0.419187052596701,
0.420981972978595,0.423860023918919,0.430824699012687,0.482805612174114,
0.509509434687927,0.521016544977097,0.523300338645433,0.524559168456589,
0.525630246915027,0.526974699096923,0.529581283887988,0.54528371603,0.551463612770259,
0.555216497853862,0.565595683086056,0.598425173069379,0.614951374796059,
0.625246303822338,0.628493163534855,0.630566086895852,0.632506942279414,
0.635049139215031,0.639347682473988,0.674733840529545,0.723911451889856,
0.733226330126461,0.735370560884082,0.736598931382085,0.737673810555959,
0.739062031216454,0.741973955552941,0.773378916617537,0.777667782332219,
0.810468023444918,0.833121868059516,0.838788741184759,0.841362599484792,
0.843301598716053,0.845127794038316,0.847667377626918,0.854292603213663,
0.910304071294489,0.934266497183649,0.945062648923812,0.947305179451994,
0.948555190850898,0.949627313461724,0.950984029300079,0.953131498578615,
0.964196586743705,1.0153361162577,1.04406147028494,1.05049807973324,1.05320752185898,
1.05516958322811,1.05696241852631,1.05982745218169,1.06671072952063,1.11985813809552,
1.14575589564192,1.15706084974852,1.15933350640645,1.16059008915057,1.16166161579937,
1.163009634232,1.16563194964916,1.18168004992619,1.1857909545577,1.20148300101392,
1.23437115886928,1.25715922870071,1.26001551649135),.UNSPECIFIED.);
#1896=B_SPLINE_CURVE_WITH_KNOTS('',3,(#183158,#183159,#183160,#183161,#183162,
#183163,#183164,#183165,#183166,#183167),.UNSPECIFIED.,.F.,.F.,(4,1,1,1,
1,1,1,4),(-22.6905949549614,-21.9744018991612,-20.9755654491994,-19.9767289992375,
-18.9778925492756,-17.9790560993137,-16.9802196493519,-16.7565928334374),
 .UNSPECIFIED.);
#1897=B_SPLINE_CURVE_WITH_KNOTS('',3,(#183168,#183169,#183170,#183171,#183172,
#183173,#183174,#183175,#183176,#183177,#183178,#183179,#183180,#183181,
#183182,#183183,#183184,#183185,#183186,#183187),.UNSPECIFIED.,.F.,.F.,
(4,2,2,2,2,2,2,2,2,4),(0.000629315580650519,0.0163202363040628,0.0544201888437156,
0.0580035127267242,0.0595138353816897,0.0606060562445949,0.0616313318818364,
0.0633718340587686,0.0680887842443331,0.0747327161871493),.UNSPECIFIED.);
#1898=B_SPLINE_CURVE_WITH_KNOTS('',3,(#183192,#183193,#183194,#183195,#183196,
#183197,#183198,#183199,#183200,#183201,#183202,#183203,#183204,#183205,
#183206,#183207,#183208,#183209,#183210,#183211,#183212,#183213,#183214,
#183215,#183216,#183217,#183218,#183219,#183220,#183221,#183222,#183223,
#183224,#183225,#183226,#183227,#183228,#183229,#183230,#183231,#183232,
#183233,#183234,#183235,#183236,#183237,#183238,#183239,#183240,#183241,
#183242,#183243,#183244,#183245,#183246,#183247,#183248,#183249,#183250,
#183251,#183252,#183253,#183254,#183255,#183256,#183257,#183258,#183259,
#183260,#183261,#183262,#183263,#183264,#183265,#183266,#183267,#183268,
#183269,#183270,#183271,#183272,#183273,#183274,#183275,#183276,#183277,
#183278,#183279,#183280,#183281,#183282,#183283,#183284,#183285,#183286,
#183287,#183288,#183289,#183290,#183291,#183292,#183293,#183294,#183295,
#183296,#183297,#183298,#183299,#183300,#183301,#183302,#183303,#183304,
#183305,#183306,#183307,#183308,#183309,#183310,#183311,#183312,#183313,
#183314,#183315,#183316,#183317,#183318,#183319,#183320,#183321,#183322,
#183323,#183324,#183325,#183326,#183327,#183328,#183329,#183330,#183331,
#183332,#183333,#183334,#183335,#183336,#183337,#183338,#183339,#183340,
#183341,#183342,#183343,#183344,#183345,#183346,#183347,#183348,#183349,
#183350,#183351,#183352,#183353,#183354,#183355,#183356,#183357,#183358,
#183359,#183360,#183361,#183362,#183363,#183364,#183365,#183366,#183367,
#183368,#183369,#183370,#183371,#183372,#183373,#183374,#183375,#183376,
#183377,#183378,#183379,#183380,#183381,#183382,#183383,#183384,#183385,
#183386,#183387,#183388,#183389,#183390,#183391,#183392,#183393,#183394,
#183395,#183396,#183397,#183398,#183399,#183400,#183401,#183402,#183403,
#183404,#183405,#183406,#183407,#183408,#183409,#183410,#183411,#183412,
#183413,#183414,#183415,#183416,#183417,#183418,#183419,#183420,#183421,
#183422,#183423,#183424,#183425,#183426,#183427,#183428,#183429,#183430,
#183431),.UNSPECIFIED.,.F.,.F.,(4,2,2,2,2,2,2,2,2,2,2,2,2,2,2,2,2,2,2,2,
2,2,2,2,2,2,2,2,2,2,2,2,2,2,2,2,2,2,2,2,2,2,2,2,2,2,2,2,2,2,2,2,2,2,2,2,
2,2,2,2,2,2,2,2,2,2,2,2,2,2,2,2,2,2,2,2,2,2,2,2,2,2,2,2,2,2,2,2,2,2,2,2,
2,2,2,2,2,2,2,2,2,2,2,2,2,2,2,2,2,2,2,2,2,2,2,2,2,2,2,4),(1.25983790857793,
1.27797720523257,1.28156303790082,1.28307395792435,1.28416643896761,1.28519182205558,
1.28693221482015,1.29164717042241,1.33205648703802,1.3339458948937,1.37777069272836,
1.38499259263956,1.387913812067,1.38971681704495,1.39167029368026,1.3943323254265,
1.40049301998838,1.42695877731456,1.46587466816546,1.47401787505932,1.49129054790315,
1.49395903095881,1.49531683613192,1.49638891725887,1.49763785070098,1.49987587301008,
1.51060187884258,1.53430546558711,1.56167740146777,1.59360713178078,1.59784660940097,
1.60037174209123,1.6023099338345,1.60439013380503,1.60766969773444,1.61825127924484,
1.63541789455111,1.68115828269663,1.6879204758484,1.70336710376258,1.70573503387373,
1.70714261744554,1.70822277246688,1.70942623007516,1.71145805126151,1.71934859563784,
1.73406464165688,1.76310434016164,1.80549060627848,1.80978360014269,1.81232430373996,
1.81426503845648,1.81633882064678,1.81958908698159,1.82991211246918,1.84650218830943,
1.8794142093178,1.89545946012091,1.89928711031461,1.91528402609327,1.91790301058041,
1.91925020518782,1.92032154387906,1.92157845326514,1.92385308013381,1.93519666654688,
1.96124611680367,2.01412103995842,2.0210210133345,2.02388855897214,2.02568168196252,
2.02764303205819,2.03034960299055,2.0367704311123,2.06537054533334,2.11662171043,
2.12774598260801,2.12989698711648,2.13125471052477,2.13232681754745,2.13357588503383,
2.13581440592864,2.1465476932325,2.17027746553897,2.22659602015694,2.23318401377596,
2.23571755929501,2.23754205871452,2.23948169940866,2.24206057070796,2.24775553250463,
2.27062223697597,2.30358524581222,2.32245679168493,2.3267697713123,2.33956211858517,
2.34180652401039,2.34319245835702,2.34426701265935,2.34549664057627,2.34764687852778,
2.35704757590243,2.40626454393015,2.44146541127269,2.44614418107161,2.44857826853674,
2.45044818795255,2.45253358762694,2.45471588495329,2.45793044457636,2.49302281158196,
2.54885369014608,2.55313420694314,2.55480687508637,2.55581911573968,2.5569212788574,
2.55848527009532,2.56239199961126,2.5815475823925,2.59336419963794),
 .UNSPECIFIED.);
#1899=B_SPLINE_CURVE_WITH_KNOTS('',3,(#183432,#183433,#183434,#183435,#183436,
#183437,#183438,#183439,#183440,#183441,#183442,#183443,#183444,#183445,
#183446,#183447,#183448,#183449,#183450,#183451,#183452,#183453,#183454,
#183455,#183456,#183457,#183458,#183459,#183460,#183461,#183462,#183463,
#183464,#183465,#183466,#183467,#183468,#183469,#183470,#183471,#183472,
#183473,#183474,#183475,#183476,#183477,#183478,#183479,#183480,#183481,
#183482,#183483,#183484,#183485,#183486,#183487,#183488,#183489,#183490,
#183491,#183492,#183493,#183494,#183495,#183496,#183497,#183498,#183499,
#183500,#183501,#183502,#183503,#183504,#183505,#183506,#183507,#183508,
#183509,#183510,#183511,#183512,#183513,#183514,#183515,#183516,#183517,
#183518,#183519,#183520,#183521,#183522,#183523,#183524,#183525,#183526,
#183527,#183528,#183529,#183530,#183531,#183532,#183533,#183534,#183535,
#183536,#183537,#183538,#183539,#183540,#183541,#183542,#183543,#183544,
#183545,#183546,#183547,#183548,#183549,#183550,#183551,#183552,#183553,
#183554,#183555,#183556,#183557,#183558,#183559,#183560,#183561,#183562,
#183563,#183564,#183565,#183566,#183567,#183568,#183569,#183570,#183571,
#183572,#183573,#183574,#183575,#183576,#183577,#183578,#183579,#183580,
#183581,#183582,#183583,#183584,#183585,#183586,#183587,#183588,#183589,
#183590,#183591,#183592,#183593,#183594,#183595,#183596,#183597,#183598,
#183599,#183600,#183601,#183602,#183603,#183604,#183605,#183606,#183607,
#183608,#183609,#183610,#183611,#183612,#183613,#183614,#183615,#183616,
#183617,#183618,#183619,#183620,#183621,#183622,#183623,#183624,#183625,
#183626,#183627,#183628,#183629,#183630,#183631,#183632,#183633,#183634,
#183635,#183636,#183637,#183638,#183639,#183640,#183641,#183642,#183643,
#183644,#183645,#183646,#183647),.UNSPECIFIED.,.F.,.F.,(4,2,2,2,2,2,2,2,
2,2,2,2,2,2,2,2,2,2,2,2,2,2,2,2,2,2,2,2,2,2,2,2,2,2,2,2,2,2,2,2,2,2,2,2,
2,2,2,2,2,2,2,2,2,2,2,2,2,2,2,2,2,2,2,2,2,2,2,2,2,2,2,2,2,2,2,2,2,2,2,2,
2,2,2,2,2,2,2,2,2,2,2,2,2,2,2,2,2,2,2,2,2,2,2,2,2,2,2,4),(0.0747327161871493,
0.112806263249665,0.136932016893629,0.151520374868938,0.160861100382372,
0.163933560938048,0.166006632969609,0.16794710999224,0.170488064463653,
0.174782832519329,0.209904538757292,0.258831792828393,0.26859796551639,
0.270773729244168,0.272008956847566,0.273082629072402,0.274459858393428,
0.277315979291488,0.30012692356418,0.345792858012144,0.362352409594568,
0.372662291999832,0.375910767549687,0.377983977490443,0.379924577789205,
0.382465685298002,0.386760693218058,0.421881873366653,0.470803718405356,
0.480580664350534,0.48275726154936,0.483992721111619,0.485066440616442,
0.486443528863192,0.489298663294989,0.512064187029572,0.524919300846613,
0.557770477962619,0.574321506103386,0.584627831901054,0.587876118415675,
0.589949431622159,0.591890285885263,0.594431952936962,0.598728415445979,
0.633929687462879,0.683101121258225,0.692593317730559,0.694750293473788,
0.69598151626546,0.697056006802251,0.698439932258856,0.700677296610982,
0.713330659266395,0.763174181018253,0.791498895283811,0.797887510368748,
0.800588778804796,0.802549308251866,0.80434376940163,0.807218000632127,
0.814157564220036,0.866538272552775,0.892970541954052,0.904410644615518,
0.906690959398448,0.907949177114371,0.909020523982913,0.910366315766807,
0.912978431743436,0.928753383487914,0.929617580563808,0.973975024025688,
1.003346825627,1.00985994589294,1.01258225926934,1.01454668941625,1.01633693092621,
1.01918752616203,1.0259831902078,1.08019676365256,1.10536228031066,1.11647832368368,
1.11874002194943,1.11999423222078,1.12106598442386,1.12241715673457,1.12505409203379,
1.14148619742741,1.19207769209147,1.2097902620344,1.22061454401318,1.2239212461215,
1.22600756770438,1.22794381133236,1.23045554869039,1.23464868172609,1.26439484972425,
1.30534135019042,1.32782242906259,1.33048602114964,1.33182494466666,1.33279298286869,
1.33401667433845,1.33613933140971,1.34515862481949,1.36314493821362,1.40835625272083),
 .UNSPECIFIED.);
#1900=B_SPLINE_CURVE_WITH_KNOTS('',3,(#183653,#183654,#183655,#183656,#183657,
#183658),.UNSPECIFIED.,.F.,.F.,(4,2,4),(2.59396194766411,2.60938231110621,
2.6684204151543),.UNSPECIFIED.);
#1901=B_SPLINE_CURVE_WITH_KNOTS('',3,(#183659,#183660,#183661,#183662,#183663,
#183664,#183665,#183666,#183667,#183668,#183669,#183670,#183671,#183672,
#183673,#183674,#183675,#183676,#183677,#183678,#183679,#183680,#183681,
#183682,#183683,#183684,#183685,#183686,#183687,#183688,#183689,#183690,
#183691,#183692,#183693,#183694,#183695,#183696,#183697,#183698,#183699,
#183700,#183701,#183702,#183703,#183704,#183705,#183706,#183707,#183708,
#183709,#183710,#183711,#183712,#183713,#183714,#183715,#183716,#183717,
#183718,#183719,#183720,#183721,#183722,#183723,#183724,#183725,#183726,
#183727,#183728,#183729,#183730,#183731,#183732,#183733,#183734,#183735,
#183736,#183737,#183738,#183739,#183740,#183741,#183742,#183743,#183744,
#183745,#183746,#183747,#183748,#183749,#183750,#183751,#183752,#183753,
#183754,#183755,#183756,#183757,#183758,#183759,#183760,#183761,#183762,
#183763,#183764,#183765,#183766,#183767,#183768,#183769,#183770,#183771,
#183772,#183773,#183774,#183775,#183776,#183777,#183778,#183779,#183780,
#183781,#183782,#183783,#183784,#183785,#183786,#183787,#183788,#183789,
#183790,#183791,#183792,#183793,#183794,#183795,#183796,#183797,#183798,
#183799,#183800,#183801,#183802,#183803,#183804,#183805,#183806,#183807,
#183808,#183809,#183810,#183811,#183812,#183813,#183814,#183815,#183816,
#183817,#183818,#183819,#183820,#183821,#183822,#183823,#183824,#183825,
#183826,#183827,#183828,#183829,#183830,#183831,#183832,#183833,#183834,
#183835,#183836,#183837,#183838,#183839,#183840,#183841,#183842,#183843,
#183844,#183845,#183846,#183847,#183848,#183849,#183850,#183851,#183852,
#183853,#183854,#183855,#183856,#183857,#183858,#183859,#183860,#183861,
#183862,#183863,#183864,#183865,#183866,#183867,#183868,#183869,#183870,
#183871,#183872,#183873,#183874,#183875,#183876,#183877,#183878,#183879,
#183880),.UNSPECIFIED.,.F.,.F.,(4,2,2,2,2,2,2,2,2,2,2,2,2,2,2,2,2,2,2,2,
2,2,2,2,2,2,2,2,2,2,2,2,2,2,2,2,2,2,2,2,2,2,2,2,2,2,2,2,2,2,2,2,2,2,2,2,
2,2,2,2,2,2,2,2,2,2,2,2,2,2,2,2,2,2,2,2,2,2,2,2,2,2,2,2,2,2,2,2,2,2,2,2,
2,2,2,2,2,2,2,2,2,2,2,2,2,2,2,2,2,2,4),(0.000810724389290951,0.00554261375580484,
0.00881069691195324,0.0102445769783141,0.011318985848088,0.0123418025241498,
0.0133650045898498,0.0148060212231952,0.0186526235771321,0.0263910153305198,
0.0811772808672639,0.107629387837393,0.113788020924836,0.116449253515829,
0.118402180529452,0.120204708031169,0.123125208371619,0.130345635359972,
0.174351807037448,0.207135137809993,0.215734594940256,0.219348857655954,
0.221296373882804,0.22257585593342,0.223774129654423,0.224825662411511,
0.226202815743788,0.229059222189351,0.265112317068062,0.29780688404151,
0.32030387335704,0.325948779676435,0.3285181613556,0.330456027760932,0.332282802427431,
0.334825834325865,0.341475778654321,0.397208499776815,0.421336622553385,
0.432176261672697,0.434420973828269,0.43567124200945,0.436742993562836,
0.438098481507766,0.440845295152296,0.459441566198162,0.508226353031946,
0.525602943175706,0.536278201585356,0.53956778574421,0.541649913854862,
0.543586834722163,0.546105943487939,0.550325687766331,0.581324838595276,
0.621242465250727,0.636423823917826,0.644481377707186,0.646527183489368,
0.647733593571336,0.648812709538806,0.650214101656203,0.652561315377136,
0.667512518906407,0.67511482761232,0.688554352914632,0.721406441682432,
0.744146843191376,0.749824902396771,0.75240052315621,0.754339504883303,
0.756164697307141,0.758701306467865,0.765309481953417,0.821463247846527,
0.845321199919284,0.856088220064211,0.858328677587908,0.859578093584948,
0.860650051457819,0.86200700293403,0.864671715982247,0.881846600474784,
0.927339625368517,0.9551961863153,0.961527955279621,0.964219336130375,0.966177888532615,
0.967974140966102,0.970859137333597,0.977865251631405,1.02920028612628,
1.05636942333767,1.06799185033315,1.07028217301201,1.07154245580033,1.07261347847955,
1.07395622287387,1.07655472432443,1.09206545116655,1.09863982300736,1.1400175365505,
1.16728220599751,1.17354198318758,1.17622110404514,1.17817754045073,1.17997659153028,
1.18287654647134,1.1899719991594,1.23960035131516,1.25983790857793),
 .UNSPECIFIED.);
#1902=B_SPLINE_CURVE_WITH_KNOTS('',3,(#183882,#183883,#183884,#183885,#183886,
#183887,#183888,#183889,#183890,#183891,#183892,#183893,#183894,#183895,
#183896,#183897,#183898,#183899,#183900,#183901,#183902,#183903,#183904,
#183905,#183906,#183907,#183908,#183909,#183910,#183911,#183912,#183913,
#183914,#183915,#183916,#183917,#183918,#183919,#183920,#183921,#183922,
#183923,#183924,#183925,#183926,#183927,#183928,#183929,#183930,#183931,
#183932,#183933,#183934,#183935,#183936,#183937,#183938,#183939,#183940,
#183941,#183942,#183943,#183944,#183945,#183946,#183947,#183948,#183949,
#183950,#183951,#183952,#183953,#183954,#183955,#183956,#183957,#183958,
#183959,#183960,#183961,#183962,#183963,#183964,#183965,#183966,#183967,
#183968,#183969,#183970,#183971,#183972,#183973,#183974,#183975,#183976,
#183977,#183978,#183979,#183980,#183981,#183982,#183983,#183984,#183985,
#183986,#183987,#183988,#183989,#183990,#183991,#183992,#183993,#183994,
#183995,#183996,#183997,#183998,#183999,#184000,#184001,#184002,#184003,
#184004,#184005,#184006,#184007,#184008,#184009,#184010,#184011,#184012,
#184013,#184014,#184015,#184016,#184017,#184018,#184019,#184020,#184021,
#184022,#184023,#184024,#184025,#184026,#184027,#184028,#184029,#184030,
#184031,#184032,#184033,#184034,#184035,#184036,#184037,#184038,#184039,
#184040,#184041,#184042,#184043,#184044,#184045,#184046,#184047,#184048,
#184049,#184050,#184051,#184052,#184053,#184054,#184055,#184056,#184057,
#184058,#184059,#184060,#184061,#184062,#184063,#184064,#184065,#184066,
#184067,#184068,#184069,#184070,#184071,#184072,#184073,#184074,#184075,
#184076,#184077,#184078,#184079,#184080,#184081,#184082,#184083,#184084,
#184085,#184086,#184087,#184088,#184089,#184090,#184091,#184092,#184093,
#184094,#184095,#184096,#184097,#184098,#184099,#184100,#184101,#184102,
#184103,#184104,#184105,#184106,#184107,#184108,#184109),.UNSPECIFIED.,
 .F.,.F.,(4,2,2,2,2,2,2,2,2,2,2,2,2,2,2,2,2,2,2,2,2,2,2,2,2,2,2,2,2,2,2,
2,2,2,2,2,2,2,2,2,2,2,2,2,2,2,2,2,2,2,2,2,2,2,2,2,2,2,2,2,2,2,2,2,2,2,2,
2,2,2,2,2,2,2,2,2,2,2,2,2,2,2,2,2,2,2,2,2,2,2,2,2,2,2,2,2,2,2,2,2,2,2,2,
2,2,2,2,2,2,2,2,2,2,4),(1.40835625272083,1.41336368806739,1.43116872566781,
1.43484842293011,1.43723220416798,1.43914781687456,1.4413267132969,1.44505177945364,
1.46045916759543,1.51179701767642,1.53947811685562,1.54238526115338,1.54377266130752,
1.54484757386111,1.546076740306,1.54822412401745,1.55758038234137,1.6068490786857,
1.64207475295534,1.64637169417152,1.6489136504204,1.65085471803946,1.65292825100875,
1.65617686359758,1.66648398593569,1.68303837202102,1.71592233387626,1.72936951776526,
1.73695626675539,1.75195389546679,1.75430351576105,1.75570578880263,1.75678524748666,
1.75799168003349,1.76003671720068,1.76808121533805,1.78322228438951,1.82293243544293,
1.85416626673713,1.85839175519206,1.86091289225587,1.86285054494295,1.8649326461682,
1.86822046079938,1.87887468072414,1.89620441513131,1.9444306171971,1.94873390689186,
1.95196293469188,1.96419552942283,1.96641049758499,1.96778768894949,1.96886155053835,
1.97009725167077,1.97227444775361,1.98205730690306,2.03095657979584,2.0660685568434,
2.07036387814959,2.0729053149221,2.07484623859035,2.0769198628265,2.08016913003967,
2.09048264193443,2.10705139361886,2.13994656134181,2.15456287475828,2.15981787996429,
2.17586545609174,2.17848752879942,2.17983542309108,2.18090685095587,2.18216332356894,
2.18443578445295,2.19574038045612,2.22163585464488,2.27473613504417,2.28161925106378,
2.28448410119294,2.28627679100996,2.28823867437865,2.29094782844773,2.29738353678552,
2.30627119379578,2.35748924472459,2.38749103980191,2.39040567361415,2.39179444617781,
2.39286940842842,2.3940974981232,2.39624034450607,2.40553570108986,2.4243798824607,
2.47057382382192,2.47203375715982,2.4910579469055,2.49481781987104,2.49722617337713,
2.4991438712783,2.50094123856844,2.50403405192422,2.51357919660978,2.52858022240595,
2.55087382072599,2.59692596171914,2.60157163495471,2.60330156075396,2.60432493251932,
2.6054188161644,2.60693747948808,2.61056863437898,2.6156799188112,2.62984817881187,
2.66748302574586),.UNSPECIFIED.);
#1903=B_SPLINE_CURVE_WITH_KNOTS('',3,(#184110,#184111,#184112,#184113,#184114,
#184115,#184116,#184117,#184118,#184119,#184120,#184121,#184122,#184123,
#184124,#184125,#184126,#184127,#184128,#184129),.UNSPECIFIED.,.F.,.F.,
(4,2,2,2,2,2,2,2,2,4),(0.000704184852116804,0.0257176022094043,0.0359848500666596,
0.0390635722060811,0.0411898678713681,0.0432710177822686,0.0452083783979804,
0.0477299820330082,0.0519581544184686,0.0751489451347217),.UNSPECIFIED.);
#1904=B_SPLINE_CURVE_WITH_KNOTS('',3,(#184134,#184135,#184136,#184137,#184138,
#184139,#184140,#184141,#184142,#184143,#184144,#184145,#184146,#184147,
#184148,#184149,#184150,#184151,#184152,#184153,#184154,#184155,#184156,
#184157,#184158,#184159,#184160,#184161,#184162,#184163,#184164,#184165,
#184166,#184167,#184168,#184169,#184170,#184171,#184172,#184173,#184174,
#184175,#184176,#184177,#184178,#184179,#184180,#184181,#184182,#184183,
#184184,#184185,#184186,#184187,#184188,#184189,#184190,#184191,#184192,
#184193,#184194,#184195,#184196,#184197,#184198,#184199,#184200,#184201,
#184202,#184203,#184204,#184205,#184206,#184207,#184208,#184209,#184210,
#184211,#184212,#184213,#184214,#184215,#184216,#184217,#184218,#184219,
#184220,#184221,#184222,#184223,#184224,#184225,#184226,#184227,#184228,
#184229,#184230,#184231,#184232,#184233,#184234,#184235,#184236,#184237,
#184238,#184239,#184240,#184241,#184242,#184243,#184244,#184245,#184246,
#184247,#184248,#184249,#184250,#184251,#184252,#184253,#184254,#184255,
#184256,#184257,#184258,#184259,#184260,#184261,#184262,#184263,#184264,
#184265,#184266,#184267,#184268,#184269,#184270,#184271,#184272,#184273,
#184274,#184275,#184276,#184277,#184278,#184279,#184280,#184281,#184282,
#184283,#184284,#184285,#184286,#184287,#184288,#184289,#184290,#184291,
#184292,#184293,#184294,#184295,#184296,#184297,#184298,#184299,#184300,
#184301,#184302,#184303,#184304,#184305,#184306,#184307,#184308,#184309,
#184310,#184311,#184312,#184313,#184314,#184315,#184316,#184317,#184318,
#184319,#184320,#184321,#184322,#184323,#184324,#184325,#184326,#184327,
#184328,#184329,#184330,#184331,#184332,#184333,#184334,#184335,#184336,
#184337,#184338,#184339,#184340,#184341,#184342,#184343,#184344,#184345,
#184346,#184347,#184348,#184349,#184350,#184351,#184352,#184353,#184354,
#184355,#184356,#184357,#184358,#184359,#184360,#184361,#184362,#184363,
#184364,#184365,#184366,#184367,#184368,#184369,#184370,#184371,#184372,
#184373,#184374,#184375,#184376,#184377,#184378,#184379,#184380,#184381,
#184382,#184383,#184384,#184385,#184386,#184387,#184388,#184389,#184390,
#184391,#184392,#184393,#184394,#184395,#184396,#184397,#184398,#184399,
#184400,#184401,#184402,#184403,#184404,#184405,#184406,#184407,#184408,
#184409),.UNSPECIFIED.,.F.,.F.,(4,2,2,2,2,2,2,2,2,2,2,2,2,2,2,2,2,2,2,2,
2,2,2,2,2,2,2,2,2,2,2,2,2,2,2,2,2,2,2,2,2,2,2,2,2,2,2,2,2,2,2,2,2,2,2,2,
2,2,2,2,2,2,2,2,2,2,2,2,2,2,2,2,2,2,2,2,2,2,2,2,2,2,2,2,2,2,2,2,2,2,2,2,
2,2,2,2,2,2,2,2,2,2,2,2,2,2,2,2,2,2,2,2,2,2,2,2,2,2,2,2,2,2,2,2,2,2,2,2,
2,2,2,2,2,2,2,2,2,4),(1.26015660703498,1.26850353839846,1.29388141845515,
1.29815223390653,1.30044982624054,1.30234294688901,1.30458374931348,1.30848301244928,
1.32439211594051,1.3346146286344,1.37390000555279,1.40248494808154,1.40539757889374,
1.4067861653548,1.40786133728485,1.40909006222754,1.41123494397423,1.42055345384096,
1.46973117631598,1.50510123298155,1.50940052081475,1.51194334691486,1.51388478037683,
1.51595841496646,1.51920658323939,1.52950721437933,1.54604634616807,1.57359384006365,
1.58973745550778,1.60082107001498,1.6150540366232,1.61737054723746,1.61876321784715,
1.61984151672186,1.62105362144081,1.62312371831444,1.63146796498687,1.64745439110005,
1.68977182301542,1.71738179358572,1.72151940303762,1.72401499119278,1.72594889825981,
1.72804276337901,1.73138310540736,1.74251617589424,1.76094094499302,1.80770403810387,
1.81238790076397,1.82704125409291,1.82937668556193,1.83077491997594,1.83185397143872,
1.83306295822877,1.83511895173284,1.84329148009806,1.85878990810227,1.90014881820821,
1.92932982664744,1.93350872854028,1.93601645369324,1.93795224668422,1.94004069592337,
1.9433563643061,1.95426036548847,1.97215678748334,2.02283065706109,2.03896711092047,
2.04159626732589,2.04294587667124,2.04401765752629,2.04527337487705,2.04754150624368,
2.05876435009312,2.08433662102447,2.13792608376044,2.14477313424653,2.14763247031026,
2.14942447106373,2.15138782627842,2.15410310544928,2.16057284687703,2.21477965760947,
2.22580484585943,2.25070462983722,2.25359339765226,2.25497732615041,2.25605200636901,
2.25728366581576,2.25944191075616,2.26894803191861,2.31809352045741,2.3532860024778,
2.35758302448765,2.36012517427007,2.36206647359919,2.36414033545589,2.36738963318007,
2.37770036072059,2.39426189888552,2.42798255702194,2.46276561958121,2.46564472786883,
2.46702673969045,2.46806957966137,2.46807433654214,2.46807900997116,2.46808360166098,
2.46808811350254,2.46809254731902,2.46809690480249,2.46810118785428,2.46810539778791,
2.46810953607837,2.4681136044994,2.46811760436237,2.46812153721469,2.46812540446117,
2.46812900140162,2.46813258499554,2.46813615516565,2.46813971186342,2.46814325546488,
2.46936716343783,2.47067885718657,2.47270356797895,2.47652077094661,2.48580997197465,
2.52380810757076,2.53846120539619,2.56559448357076,2.5697198083356,2.57221178784583,
2.57414515533493,2.57624069134386,2.57958858900748,2.59079256646039,2.59396194766411),
 .UNSPECIFIED.);
#1905=B_SPLINE_CURVE_WITH_KNOTS('',3,(#184410,#184411,#184412,#184413,#184414,
#184415,#184416,#184417,#184418,#184419,#184420,#184421,#184422,#184423,
#184424,#184425,#184426,#184427,#184428,#184429,#184430,#184431,#184432,
#184433,#184434,#184435,#184436,#184437,#184438,#184439,#184440,#184441,
#184442,#184443,#184444,#184445,#184446,#184447,#184448,#184449,#184450,
#184451,#184452,#184453,#184454,#184455,#184456,#184457,#184458,#184459,
#184460,#184461,#184462,#184463,#184464,#184465,#184466,#184467,#184468,
#184469,#184470,#184471,#184472,#184473,#184474,#184475,#184476,#184477,
#184478,#184479,#184480,#184481,#184482,#184483,#184484,#184485,#184486,
#184487,#184488,#184489,#184490,#184491,#184492,#184493,#184494,#184495,
#184496,#184497,#184498,#184499,#184500,#184501,#184502,#184503,#184504,
#184505,#184506,#184507,#184508,#184509,#184510,#184511,#184512,#184513,
#184514,#184515,#184516,#184517,#184518,#184519,#184520,#184521,#184522,
#184523,#184524,#184525,#184526,#184527,#184528,#184529,#184530,#184531,
#184532,#184533,#184534,#184535,#184536,#184537,#184538,#184539,#184540,
#184541,#184542,#184543,#184544,#184545,#184546,#184547,#184548,#184549,
#184550,#184551,#184552,#184553,#184554,#184555,#184556,#184557,#184558,
#184559,#184560,#184561,#184562,#184563,#184564,#184565,#184566,#184567,
#184568,#184569,#184570,#184571,#184572,#184573,#184574,#184575,#184576,
#184577,#184578,#184579,#184580,#184581,#184582,#184583,#184584,#184585,
#184586,#184587,#184588,#184589,#184590,#184591,#184592,#184593,#184594,
#184595,#184596,#184597,#184598,#184599,#184600,#184601,#184602,#184603,
#184604,#184605,#184606,#184607,#184608,#184609,#184610,#184611,#184612,
#184613,#184614,#184615,#184616,#184617,#184618,#184619,#184620,#184621,
#184622,#184623,#184624,#184625,#184626,#184627,#184628,#184629,#184630,
#184631,#184632,#184633,#184634,#184635,#184636,#184637,#184638,#184639),
 .UNSPECIFIED.,.F.,.F.,(4,2,2,2,2,2,2,2,2,2,2,2,2,2,2,2,2,2,2,2,2,2,2,2,
2,2,2,2,2,2,2,2,2,2,2,2,2,2,2,2,2,2,2,2,2,2,2,2,2,2,2,2,2,2,2,2,2,2,2,2,
2,2,2,2,2,2,2,2,2,2,2,2,2,2,2,2,2,2,2,2,2,2,2,2,2,2,2,2,2,2,2,2,2,2,2,2,
2,2,2,2,2,2,2,2,2,2,2,2,2,2,2,2,2,2,4),(0.0751489451347217,0.0833507687398273,
0.108693897814586,0.136627086573777,0.145910886645299,0.148052581554333,
0.149280244099893,0.150354989768126,0.151743679457158,0.153997484253236,
0.166976862044332,0.188667672851665,0.215384456391813,0.236981735410283,
0.245198580224,0.251207962177669,0.253835108106743,0.25579166492443,0.257590154255876,
0.260487716487645,0.267569839542336,0.317778483894999,0.355565284018007,
0.359164609079005,0.360677739990485,0.361770526142713,0.362795167290526,
0.364532111062224,0.369224987747128,0.410119178514221,0.4567277765047,0.463120318208575,
0.465821987649755,0.467782348658663,0.469576338621285,0.472449122864454,
0.479381619562274,0.531831153367774,0.558205057179414,0.569629706952713,
0.571908878575761,0.573166723471649,0.574237908965008,0.575583696383888,
0.578196384936595,0.594048605625068,0.598801103315708,0.614070826201948,
0.646946930371511,0.663528806028483,0.673848987832411,0.677098794684803,
0.679172394756504,0.681113037550354,0.683653735258197,0.687947007613558,
0.730347335586221,0.759403786114085,0.774125645839017,0.782017432494795,
0.784049295302067,0.785252716774208,0.786332803687113,0.787740237111621,
0.790107777879002,0.805548576264205,0.812259402678407,0.826060078339225,
0.858920786798176,0.875483084096869,0.88579453543023,0.889043430538638,
0.891116890278173,0.893057711776927,0.895599090725547,0.89989451662427,
0.935013736138574,0.98392289543762,0.993722764407131,0.995901100414189,
0.997137029899902,0.998210827162394,0.99958758320526,1.00244054459879,1.02510735550418,
1.0380664302586,1.07092235863773,1.08747644518285,1.09778448107669,1.10103320308503,
1.10310676938518,1.10504784309833,1.10758977231665,1.11188662146474,1.14708338049787,
1.19623182845181,1.20575825710308,1.20791781881272,1.20914969868785,1.21022423315029,
1.21160751962747,1.21384248950938,1.22644680162857,1.23298162269474,1.2381153243991,
1.27817836248789,1.30768223981042,1.31209267260043,1.3144196120831,1.31614670947385,
1.31830315004177,1.32192599615574,1.33437679389053,1.38533776653531,1.40863964716442),
 .UNSPECIFIED.);
#1906=B_SPLINE_CURVE_WITH_KNOTS('',3,(#184645,#184646,#184647,#184648,#184649,
#184650,#184651,#184652),.UNSPECIFIED.,.F.,.F.,(4,2,2,4),(2.59337744564721,
2.59680650631764,2.61639715086674,2.66756143788907),.UNSPECIFIED.);
#1907=B_SPLINE_CURVE_WITH_KNOTS('',3,(#184653,#184654,#184655,#184656,#184657,
#184658,#184659,#184660,#184661,#184662,#184663,#184664,#184665,#184666,
#184667,#184668,#184669,#184670,#184671,#184672,#184673,#184674,#184675,
#184676,#184677,#184678,#184679,#184680,#184681,#184682,#184683,#184684,
#184685,#184686,#184687,#184688,#184689,#184690,#184691,#184692,#184693,
#184694,#184695,#184696,#184697,#184698,#184699,#184700,#184701,#184702,
#184703,#184704,#184705,#184706,#184707,#184708,#184709,#184710,#184711,
#184712,#184713,#184714,#184715,#184716,#184717,#184718,#184719,#184720,
#184721,#184722,#184723,#184724,#184725,#184726,#184727,#184728,#184729,
#184730,#184731,#184732,#184733,#184734,#184735,#184736,#184737,#184738,
#184739,#184740,#184741,#184742,#184743,#184744,#184745,#184746,#184747,
#184748,#184749,#184750,#184751,#184752,#184753,#184754,#184755,#184756,
#184757,#184758,#184759,#184760,#184761,#184762,#184763,#184764,#184765,
#184766,#184767,#184768,#184769,#184770,#184771,#184772,#184773,#184774,
#184775,#184776,#184777,#184778,#184779,#184780,#184781,#184782,#184783,
#184784,#184785,#184786,#184787,#184788,#184789,#184790,#184791,#184792,
#184793,#184794,#184795,#184796,#184797,#184798,#184799,#184800,#184801,
#184802,#184803,#184804,#184805,#184806,#184807,#184808,#184809,#184810,
#184811,#184812,#184813,#184814,#184815,#184816,#184817,#184818,#184819,
#184820,#184821,#184822,#184823,#184824,#184825,#184826,#184827,#184828,
#184829,#184830,#184831,#184832,#184833,#184834,#184835,#184836,#184837,
#184838,#184839,#184840,#184841,#184842,#184843,#184844,#184845,#184846,
#184847,#184848,#184849,#184850,#184851,#184852,#184853,#184854,#184855,
#184856,#184857,#184858,#184859,#184860,#184861,#184862,#184863,#184864,
#184865,#184866,#184867,#184868,#184869,#184870,#184871,#184872,#184873,
#184874,#184875,#184876),.UNSPECIFIED.,.F.,.F.,(4,2,2,2,2,2,2,2,2,2,2,2,
2,2,2,2,2,2,2,2,2,2,2,2,2,2,2,2,2,2,2,2,2,2,2,2,2,2,2,2,2,2,2,2,2,2,2,2,
2,2,2,2,2,2,2,2,2,2,2,2,2,2,2,2,2,2,2,2,2,2,2,2,2,2,2,2,2,2,2,2,2,2,2,2,
2,2,2,2,2,2,2,2,2,2,2,2,2,2,2,2,2,2,2,2,2,2,2,2,2,2,2,4),(0.000768636763620859,
0.0217315066625405,0.0248344419133145,0.026970678143598,0.0287699104987455,
0.030685112795253,0.0330691762509115,0.0367508368038254,0.0545959714040407,
0.0730111911955766,0.121979341411483,0.131697019623042,0.133869453884699,
0.135103947685483,0.13617772341325,0.137556055272068,0.140417804717059,
0.176399538266315,0.20912347261868,0.225523292957851,0.232324810710104,
0.23749883879562,0.239968098028527,0.241807521593055,0.243632198876294,
0.246166562549093,0.252759959465985,0.30904444772813,0.341534533561398,
0.345079265193333,0.346583133134812,0.347674383575492,0.348701702253464,
0.350452015143498,0.355232321612756,0.391152806185594,0.39739207199896,
0.442580350157967,0.44899616353931,0.451701928678007,0.453663173029819,
0.455456532518391,0.458325170388865,0.465231446369641,0.518057677823919,
0.5441731883724,0.555533049805055,0.557808688954534,0.559065841323031,0.560137198814906,
0.561484171278437,0.56410200378966,0.58007672594858,0.585034177782859,0.629903192358926,
0.64841696001026,0.659588891152749,0.662932982927637,0.665027435070619,
0.666960685637237,0.669453750491491,0.673583575738223,0.700904603771456,
0.743187692304861,0.759434473118696,0.767867973449621,0.769945078183847,
0.771158612823763,0.772236373949629,0.773625993740701,0.775932507385694,
0.789974982568318,0.791314807245637,0.798324935592705,0.812001368770075,
0.84486321961538,0.861425190092134,0.871736702264145,0.874985757285821,
0.877059352906881,0.87900032535612,0.881541936250879,0.885837831041215,
0.920971040899617,0.969918659955791,0.979677946062808,0.981853622208183,
0.983089023191742,0.984162989001907,0.98554078169571,0.988398713743108,
1.01125863261046,1.02402504859358,1.056881633485,1.07343480107024,1.08374263051261,
1.08699148230587,1.08906517828756,1.09100640630897,1.09354858510047,1.09784596261914,
1.13306155671959,1.1822681476552,1.19173242436896,1.19388770653724,1.19511870002955,
1.19619346812021,1.19757837922565,1.19981856865074,1.21252021657982,1.23489839246917,
1.26015660703498),.UNSPECIFIED.);
#1908=B_SPLINE_CURVE_WITH_KNOTS('',3,(#184878,#184879,#184880,#184881,#184882,
#184883,#184884,#184885,#184886,#184887,#184888,#184889,#184890,#184891,
#184892,#184893,#184894,#184895,#184896,#184897,#184898,#184899,#184900,
#184901,#184902,#184903,#184904,#184905,#184906,#184907,#184908,#184909,
#184910,#184911,#184912,#184913,#184914,#184915,#184916,#184917,#184918,
#184919,#184920,#184921,#184922,#184923,#184924,#184925,#184926,#184927,
#184928,#184929,#184930,#184931,#184932,#184933,#184934,#184935,#184936,
#184937,#184938,#184939,#184940,#184941,#184942,#184943,#184944,#184945,
#184946,#184947,#184948,#184949,#184950,#184951,#184952,#184953,#184954,
#184955,#184956,#184957,#184958,#184959,#184960,#184961,#184962,#184963,
#184964,#184965,#184966,#184967,#184968,#184969,#184970,#184971,#184972,
#184973,#184974,#184975,#184976,#184977,#184978,#184979,#184980,#184981,
#184982,#184983,#184984,#184985,#184986,#184987,#184988,#184989,#184990,
#184991,#184992,#184993,#184994,#184995,#184996,#184997,#184998,#184999,
#185000,#185001,#185002,#185003,#185004,#185005,#185006,#185007,#185008,
#185009,#185010,#185011,#185012,#185013,#185014,#185015,#185016,#185017,
#185018,#185019,#185020,#185021,#185022,#185023,#185024,#185025,#185026,
#185027,#185028,#185029,#185030,#185031,#185032,#185033,#185034,#185035,
#185036,#185037,#185038,#185039,#185040,#185041,#185042,#185043,#185044,
#185045,#185046,#185047,#185048,#185049,#185050,#185051,#185052,#185053,
#185054,#185055,#185056,#185057,#185058,#185059,#185060,#185061,#185062,
#185063,#185064,#185065,#185066,#185067,#185068,#185069,#185070,#185071,
#185072,#185073,#185074,#185075,#185076,#185077,#185078,#185079,#185080,
#185081,#185082,#185083,#185084,#185085,#185086,#185087,#185088,#185089,
#185090,#185091,#185092,#185093,#185094,#185095,#185096,#185097),
 .UNSPECIFIED.,.F.,.F.,(4,2,2,2,2,2,2,2,2,2,2,2,2,2,2,2,2,2,2,2,2,2,2,2,
2,2,2,2,2,2,2,2,2,2,2,2,2,2,2,2,2,2,2,2,2,2,2,2,2,2,2,2,2,2,2,2,2,2,2,2,
2,2,2,2,2,2,2,2,2,2,2,2,2,2,2,2,2,2,2,2,2,2,2,2,2,2,2,2,2,2,2,2,2,2,2,2,
2,2,2,2,2,2,2,2,2,2,2,2,2,4),(1.40863964716442,1.41654764256288,1.41946083579173,
1.42084949652186,1.42192463669879,1.4231532255005,1.42529763564206,1.43461047793079,
1.48376965084431,1.51916016469688,1.52345953256328,1.52600232681551,1.52794369037978,
1.53001720613691,1.53326509608718,1.54356406874418,1.56009980019928,1.59297023326031,
1.60449595099036,1.61425420981712,1.61606748499759,1.62921211557533,1.63147488928389,
1.63286652026671,1.63394190601275,1.63516848294114,1.63730403115457,1.6464965067669,
1.66501716992407,1.70914927550554,1.7317840423409,1.73573479484222,1.73820143199043,
1.74012569885294,1.7422544710342,1.74575265982184,1.75846526716016,1.780743468298,
1.82624897292974,1.82856531591742,1.84126738070175,1.8435075189208,1.84489236067264,
1.84596705461519,1.8471979493487,1.84935301183245,1.85881590293729,1.90799408650132,
1.94319456261665,1.94749136408763,1.95003334092667,1.95197448372881,1.95404815465521,
1.95729710371859,1.96760630754901,1.98416500105289,2.01705344523302,2.05268901962376,
2.05555268303099,2.05693160328613,2.05800567766868,2.05924034322329,2.06141265659592,
2.07112319591955,2.12008653296455,2.15522023941421,2.15951603917115,2.1620576796872,
2.16399871326019,2.16607241060743,2.16932169986364,2.17963450169365,2.19620137045321,
2.22909593278143,2.26470526831109,2.26757139958074,2.26895077443178,2.27002485924053,
2.27125914938986,2.27342987863855,2.28311821756389,2.33209838589604,2.36723676947822,
2.37153249383134,2.37407406628394,2.37601503437213,2.37808864866394,2.38133778043728,
2.39164985193077,2.40821532813543,2.47085486389423,2.47221620671777,2.47838974893803,
2.48032809473012,2.4815108796201,2.48254253023337,2.48395558070157,2.48697057165287,
2.49106866309595,2.50134681013531,2.52416875318152,2.57588013443217,2.58286385829124,
2.58574568151114,2.58754174992021,2.58950153779053,2.59219722308898,2.59855126109664,
2.62658804342393,2.66827829265055),.UNSPECIFIED.);
#1909=B_SPLINE_CURVE_WITH_KNOTS('',3,(#185098,#185099,#185100,#185101,#185102,
#185103,#185104,#185105,#185106,#185107,#185108,#185109,#185110),
 .UNSPECIFIED.,.F.,.F.,(4,3,3,3,4),(-48.1740290121606,-48.0708041571688,
-47.9674104081966,-47.94414959817,-47.8233361836797),.UNSPECIFIED.);
#1910=B_SPLINE_CURVE_WITH_KNOTS('',3,(#185115,#185116,#185117,#185118,#185119,
#185120,#185121,#185122,#185123,#185124,#185125,#185126,#185127,#185128,
#185129,#185130,#185131,#185132,#185133,#185134,#185135,#185136,#185137,
#185138,#185139,#185140,#185141,#185142,#185143,#185144,#185145,#185146,
#185147,#185148,#185149,#185150,#185151,#185152,#185153,#185154,#185155,
#185156,#185157,#185158,#185159,#185160,#185161,#185162,#185163,#185164,
#185165,#185166,#185167,#185168,#185169,#185170,#185171,#185172,#185173,
#185174,#185175,#185176,#185177,#185178,#185179,#185180,#185181,#185182,
#185183,#185184,#185185,#185186,#185187,#185188,#185189,#185190,#185191,
#185192,#185193,#185194,#185195,#185196,#185197,#185198,#185199,#185200,
#185201,#185202,#185203,#185204,#185205,#185206,#185207,#185208,#185209,
#185210,#185211,#185212,#185213,#185214,#185215,#185216,#185217,#185218,
#185219,#185220,#185221,#185222,#185223,#185224,#185225,#185226,#185227,
#185228,#185229,#185230,#185231,#185232,#185233,#185234,#185235,#185236,
#185237,#185238,#185239,#185240,#185241,#185242,#185243,#185244,#185245,
#185246,#185247,#185248,#185249,#185250,#185251,#185252,#185253,#185254,
#185255,#185256,#185257,#185258,#185259,#185260,#185261,#185262,#185263,
#185264,#185265,#185266,#185267,#185268,#185269,#185270,#185271,#185272,
#185273,#185274,#185275,#185276,#185277,#185278,#185279,#185280,#185281,
#185282,#185283,#185284,#185285,#185286,#185287,#185288,#185289,#185290,
#185291,#185292,#185293,#185294,#185295,#185296,#185297,#185298,#185299,
#185300,#185301,#185302,#185303,#185304,#185305,#185306,#185307,#185308,
#185309,#185310,#185311,#185312,#185313,#185314,#185315,#185316,#185317,
#185318,#185319,#185320,#185321,#185322,#185323,#185324,#185325,#185326,
#185327,#185328,#185329,#185330,#185331,#185332,#185333,#185334,#185335,
#185336,#185337,#185338,#185339,#185340,#185341,#185342,#185343,#185344,
#185345,#185346,#185347,#185348,#185349,#185350),.UNSPECIFIED.,.F.,.F.,
(4,2,2,2,2,2,2,2,2,2,2,2,2,2,2,2,2,2,2,2,2,2,2,2,2,2,2,2,2,2,2,2,2,2,2,
2,2,2,2,2,2,2,2,2,2,2,2,2,2,2,2,2,2,2,2,2,2,2,2,2,2,2,2,2,2,2,2,2,2,2,2,
2,2,2,2,2,2,2,2,2,2,2,2,2,2,2,2,2,2,2,2,2,2,2,2,2,2,2,2,2,2,2,2,2,2,2,2,
2,2,2,2,2,2,2,2,2,2,4),(1.25968336163638,1.28150381246531,1.30395448572161,
1.31433170933636,1.31654811413045,1.31779240001811,1.31886512414195,1.32022971845643,
1.32240312854682,1.33389982900217,1.38263541667828,1.4158386985878,1.42010255276132,
1.42263484404187,1.42457426449047,1.42665161975916,1.42991793052054,1.44038099252285,
1.45728194656261,1.49511048235499,1.52518582864636,1.52810042018771,1.52948919693211,
1.53056417361026,1.5317922923127,1.53393521864119,1.54323137459793,1.5620779165218,
1.60247839108949,1.61474048513036,1.62934631863552,1.63313459603982,1.63534958558466,
1.63726184492923,1.63959687495713,1.64404679877848,1.67495955683427,1.72180673060197,
1.73760386952349,1.74021635035163,1.74156223435342,1.74263360368595,1.74389179423334,
1.74617191280761,1.75760854005322,1.78402413656162,1.83638761534834,1.8433260673072,
1.84620014829443,1.84799460847972,1.84995521711348,1.85265673353905,1.85904657224156,
1.88738472843888,1.93728359451395,1.94991432471917,1.95215062266111,1.95353426062917,
1.95460877032405,1.95584029620597,1.95799845335825,1.96750651575542,2.01664165675908,
2.05182794795962,2.05612430967836,2.05866607222441,2.0606070777984,2.06268062773747,
2.06592944071323,2.07623866340765,2.09279781615963,2.12568535844249,2.13955046141776,
2.14611527770527,2.16166393842342,2.16426431072071,2.16560753805181,2.16667868913047,
2.16793882946592,2.17022813003496,2.18182972273794,2.20890969275392,2.26033572295614,
2.26733473695747,2.27021873446957,2.27201493643966,2.27397389543504,2.27666666692741,
2.28300556590808,2.31092215394589,2.35691488170998,2.35827699595489,2.36020818559394,
2.37383569611647,2.37612212493758,2.37750582803373,2.37858284733383,2.37979989146837,
2.38189279084592,2.39052515500643,2.40734999387028,2.46578858300041,2.47791139323761,
2.48149830216692,2.48364647036996,2.48552293806941,2.48788387304251,2.49249150159489,
2.49839596174534,2.51181620654956,2.53423713378931,2.58327534874353,2.58750372343543,
2.58916795054713,2.5901785912019,2.59128218578855,2.59285357572233,2.59337744564721),
 .UNSPECIFIED.);
#1911=B_SPLINE_CURVE_WITH_KNOTS('',3,(#185352,#185353,#185354,#185355,#185356,
#185357,#185358,#185359,#185360,#185361,#185362,#185363,#185364,#185365,
#185366,#185367,#185368,#185369,#185370,#185371,#185372,#185373,#185374,
#185375,#185376,#185377,#185378,#185379,#185380,#185381,#185382,#185383,
#185384,#185385,#185386,#185387,#185388,#185389,#185390,#185391,#185392,
#185393,#185394,#185395,#185396,#185397,#185398,#185399,#185400,#185401,
#185402,#185403,#185404,#185405,#185406,#185407,#185408,#185409,#185410,
#185411,#185412,#185413,#185414,#185415,#185416,#185417,#185418,#185419,
#185420,#185421,#185422,#185423,#185424,#185425,#185426,#185427,#185428,
#185429,#185430,#185431,#185432,#185433,#185434,#185435,#185436,#185437,
#185438,#185439,#185440,#185441,#185442,#185443,#185444,#185445,#185446,
#185447,#185448,#185449,#185450,#185451,#185452,#185453,#185454,#185455,
#185456,#185457,#185458,#185459,#185460,#185461,#185462,#185463,#185464,
#185465,#185466,#185467,#185468,#185469,#185470,#185471,#185472,#185473,
#185474,#185475,#185476,#185477,#185478,#185479,#185480,#185481,#185482,
#185483,#185484,#185485,#185486,#185487,#185488,#185489,#185490,#185491,
#185492,#185493,#185494,#185495,#185496,#185497,#185498,#185499,#185500,
#185501,#185502,#185503,#185504,#185505,#185506,#185507,#185508,#185509,
#185510,#185511,#185512,#185513,#185514,#185515,#185516,#185517,#185518,
#185519,#185520,#185521,#185522,#185523,#185524,#185525,#185526,#185527,
#185528,#185529),.UNSPECIFIED.,.F.,.F.,(4,3,3,3,3,3,3,3,3,3,3,3,3,3,3,3,
3,3,3,3,3,3,3,3,3,3,3,3,3,3,3,3,3,3,3,3,3,3,3,3,3,3,3,3,3,3,3,3,3,3,3,3,
3,3,3,3,3,3,3,4),(-54.1065214908593,-53.9371682979412,-53.8337735608932,
-53.7305322787781,-53.6274123133857,-53.5243577451767,-53.4213345368189,
-53.3183086941465,-53.2151759273683,-53.1119868359584,-53.0086148425767,
-52.9383318479793,-52.8349371109314,-52.7316958288165,-52.6285758634243,
-52.5255212952155,-52.4224980868578,-52.3194722441853,-52.2163394774073,
-52.1131503859976,-52.009778392616,-51.9394953980175,-51.8361006609696,
-51.7328593788546,-51.6297394134623,-51.5266848452534,-51.4236616368957,
-51.3206357942232,-51.2175030274452,-51.1143139360354,-51.0109419426538,
-50.9406589480556,-50.8372642110076,-50.7340229288926,-50.6309029635003,
-50.5278483952913,-50.4248251869335,-50.321799344261,-50.2186665774828,
-50.115477486073,-50.0121054926913,-49.9418224980937,-49.8384277610458,
-49.7351864789307,-49.6320665135384,-49.5290119453295,-49.4259887369717,
-49.3229628942992,-49.2198301275211,-49.1166410361113,-49.0132690427297,
-48.9429860481318,-48.8396205066968,-48.7363953136982,-48.6332762150935,
-48.5302290794639,-48.4271932051552,-48.3241646395655,-48.2210652727443,
-48.1740290121606),.UNSPECIFIED.);
#1912=B_SPLINE_CURVE_WITH_KNOTS('',3,(#185530,#185531,#185532,#185533),
 .UNSPECIFIED.,.F.,.F.,(4,4),(-54.4565130283295,-54.1065275196936),
 .UNSPECIFIED.);
#1913=B_SPLINE_CURVE_WITH_KNOTS('',3,(#185539,#185540,#185541,#185542,#185543,
#185544,#185545,#185546,#185547,#185548,#185549,#185550,#185551,#185552,
#185553,#185554,#185555,#185556,#185557,#185558),.UNSPECIFIED.,.F.,.F.,
(4,2,2,2,2,2,2,2,2,4),(2.59313914980931,2.59886472833631,2.60312141898723,
2.60565120851499,2.60758972885503,2.60966711125076,2.61293555061346,2.61673849141341,
2.62400252838434,2.66762635786377),.UNSPECIFIED.);
#1914=B_SPLINE_CURVE_WITH_KNOTS('',3,(#185559,#185560,#185561,#185562,#185563,
#185564,#185565,#185566,#185567,#185568,#185569,#185570,#185571,#185572,
#185573,#185574,#185575,#185576,#185577,#185578,#185579,#185580,#185581,
#185582,#185583,#185584,#185585,#185586,#185587,#185588,#185589,#185590,
#185591,#185592,#185593,#185594,#185595,#185596,#185597,#185598,#185599,
#185600,#185601,#185602,#185603,#185604,#185605,#185606,#185607,#185608,
#185609,#185610,#185611,#185612,#185613,#185614,#185615,#185616,#185617,
#185618,#185619,#185620,#185621,#185622,#185623,#185624,#185625,#185626,
#185627,#185628,#185629,#185630,#185631,#185632,#185633,#185634,#185635,
#185636,#185637,#185638,#185639,#185640,#185641,#185642,#185643,#185644,
#185645,#185646,#185647,#185648,#185649,#185650,#185651,#185652,#185653,
#185654,#185655,#185656,#185657,#185658,#185659,#185660,#185661,#185662,
#185663,#185664,#185665,#185666,#185667,#185668,#185669,#185670,#185671,
#185672,#185673,#185674,#185675,#185676,#185677,#185678,#185679,#185680,
#185681,#185682,#185683,#185684,#185685,#185686,#185687,#185688,#185689,
#185690,#185691,#185692,#185693,#185694,#185695,#185696,#185697,#185698,
#185699,#185700,#185701,#185702,#185703,#185704,#185705,#185706,#185707,
#185708,#185709,#185710,#185711,#185712,#185713,#185714,#185715,#185716,
#185717,#185718,#185719,#185720,#185721,#185722,#185723,#185724,#185725,
#185726,#185727,#185728,#185729,#185730,#185731,#185732,#185733,#185734,
#185735,#185736,#185737,#185738,#185739,#185740,#185741,#185742,#185743,
#185744,#185745,#185746,#185747,#185748,#185749,#185750,#185751,#185752,
#185753,#185754,#185755,#185756,#185757,#185758,#185759,#185760,#185761,
#185762,#185763,#185764,#185765,#185766,#185767,#185768,#185769,#185770,
#185771,#185772),.UNSPECIFIED.,.F.,.F.,(4,2,2,2,2,2,2,2,2,2,2,2,2,2,2,2,
2,2,2,2,2,2,2,2,2,2,2,2,2,2,2,2,2,2,2,2,2,2,2,2,2,2,2,2,2,2,2,2,2,2,2,2,
2,2,2,2,2,2,2,2,2,2,2,2,2,2,2,2,2,2,2,2,2,2,2,2,2,2,2,2,2,2,2,2,2,2,2,2,
2,2,2,2,2,2,2,2,2,2,2,2,2,2,2,2,2,2,4),(0.00064999401870814,0.0375152740774843,
0.0412926072787783,0.0433020348222845,0.0446072165208979,0.0458444201689322,
0.0469177328032517,0.0482917920573788,0.0511320607526068,0.0879797143108778,
0.109399231159625,0.136182509301837,0.146436109229218,0.149706965971948,
0.151785053864551,0.153723653894635,0.156252719855537,0.160506384817164,
0.193189314060769,0.222561939900857,0.244175730037096,0.254295425612179,
0.256485313796723,0.257733442726415,0.258805446753902,0.260163935545637,
0.262836118809076,0.280220611714519,0.329264880991464,0.347306199028025,
0.354573879979304,0.360002618875832,0.36256780699064,0.364505140438897,
0.366333350100077,0.368881496653483,0.375563659495922,0.430964785842751,
0.455317985223457,0.466218325466524,0.46846680960563,0.469717953032539,
0.470789700695349,0.472144217413519,0.474885907083682,0.493327487968013,
0.537460170432788,0.565331791001386,0.571665310121053,0.574356949408836,
0.576315511294048,0.578111648649546,0.580996188318186,0.58799980762993,
0.639384966729156,0.666515578373941,0.678128416282107,0.680418165073668,
0.681678304585031,0.682749309311691,0.684092162770366,0.686691258230314,
0.702217026171755,0.708760852023979,0.7226338679729,0.75549393192625,0.772056435613488,
0.782367860376191,0.785616664699219,0.787690046705758,0.789630781543226,
0.792172026961885,0.796467182234275,0.831578294062515,0.880465431901704,
0.890288604243727,0.892468461492535,0.89370469305999,0.894778394330742,
0.896154559272692,0.899004689366724,0.935374535901499,0.989163003036879,
0.995619057843842,0.998331625955218,1.00029412019574,1.00208609363388,1.00494701982904,
1.01180629779494,1.06524490606319,1.09093514883092,1.1021865449968,1.10445596255679,
1.10571177114402,1.106783255761,1.10813200888855,1.11075807436306,1.12692226978114,
1.17758026273599,1.20199422941898,1.20789424776203,1.21051031179204,1.21245601008353,
1.21427040670099,1.21676501607254,1.22311486349749,1.25968336163638),
 .UNSPECIFIED.);
#1915=B_SPLINE_CURVE_WITH_KNOTS('',3,(#185774,#185775,#185776,#185777,#185778,
#185779,#185780,#185781,#185782,#185783),.UNSPECIFIED.,.F.,.F.,(4,1,1,1,
1,1,1,4),(-60.3897037700523,-59.9301869977125,-58.9313505477506,-57.9325140977887,
-56.9336776478268,-55.934841197865,-54.9360047479031,-54.4565130283295),
 .UNSPECIFIED.);
#1916=B_SPLINE_CURVE_WITH_KNOTS('',3,(#185784,#185785,#185786,#185787,#185788,
#185789,#185790,#185791,#185792,#185793,#185794,#185795,#185796,#185797,
#185798,#185799,#185800,#185801),.UNSPECIFIED.,.F.,.F.,(4,2,2,2,2,2,2,2,
4),(0.000658789691829873,0.0033297019412485,0.00592165923435953,0.00778879714723288,
0.00964368964025443,0.0114909186427276,0.0146445374997109,0.023361496180258,
0.0750717851778821),.UNSPECIFIED.);
#1917=B_SPLINE_CURVE_WITH_KNOTS('',3,(#185806,#185807,#185808,#185809,#185810,
#185811,#185812,#185813,#185814,#185815,#185816,#185817,#185818,#185819,
#185820,#185821,#185822,#185823,#185824,#185825,#185826,#185827,#185828,
#185829,#185830,#185831,#185832,#185833,#185834,#185835,#185836,#185837,
#185838,#185839,#185840,#185841,#185842,#185843,#185844,#185845,#185846,
#185847,#185848,#185849,#185850,#185851,#185852,#185853,#185854,#185855,
#185856,#185857,#185858,#185859,#185860,#185861,#185862,#185863,#185864,
#185865,#185866,#185867,#185868,#185869,#185870,#185871,#185872,#185873,
#185874,#185875,#185876,#185877,#185878,#185879,#185880,#185881,#185882,
#185883,#185884,#185885,#185886,#185887,#185888,#185889,#185890,#185891,
#185892,#185893,#185894,#185895,#185896,#185897,#185898,#185899,#185900,
#185901,#185902,#185903,#185904,#185905,#185906,#185907,#185908,#185909,
#185910,#185911,#185912,#185913,#185914,#185915,#185916,#185917,#185918,
#185919,#185920,#185921,#185922,#185923,#185924,#185925,#185926,#185927,
#185928,#185929,#185930,#185931,#185932,#185933,#185934,#185935,#185936,
#185937,#185938,#185939,#185940,#185941,#185942,#185943,#185944,#185945,
#185946,#185947,#185948,#185949,#185950,#185951,#185952,#185953,#185954,
#185955,#185956,#185957,#185958,#185959,#185960,#185961,#185962,#185963,
#185964,#185965,#185966,#185967,#185968,#185969,#185970,#185971,#185972,
#185973,#185974,#185975,#185976,#185977,#185978,#185979,#185980,#185981,
#185982,#185983,#185984,#185985,#185986,#185987,#185988,#185989,#185990,
#185991,#185992,#185993,#185994,#185995,#185996,#185997,#185998,#185999,
#186000,#186001,#186002,#186003,#186004,#186005,#186006,#186007,#186008,
#186009,#186010,#186011,#186012,#186013,#186014,#186015,#186016,#186017,
#186018,#186019,#186020,#186021,#186022,#186023),.UNSPECIFIED.,.F.,.F.,
(4,2,2,2,2,2,2,2,2,2,2,2,2,2,2,2,2,2,2,2,2,2,2,2,2,2,2,2,2,2,2,2,2,2,2,
2,2,2,2,2,2,2,2,2,2,2,2,2,2,2,2,2,2,2,2,2,2,2,2,2,2,2,2,2,2,2,2,2,2,2,2,
2,2,2,2,2,2,2,2,2,2,2,2,2,2,2,2,2,2,2,2,2,2,2,2,2,2,2,2,2,2,2,2,2,2,2,2,
2,4),(1.25981860719964,1.28582891022361,1.32659467423898,1.33166059105053,
1.33412005612525,1.33604290774328,1.33817439093442,1.34168688904338,1.35456200426643,
1.37726280817133,1.41585026003799,1.42084444542092,1.43685056924709,1.43946977576748,
1.4408168819241,1.44188804366973,1.44314462188987,1.44541833526764,1.45675091337238,
1.48276027920743,1.53567696855932,1.54257189208843,1.54543830569257,1.54723100163399,
1.54919211027279,1.55189876163002,1.55832173773744,1.58694424906269,1.63822351505355,
1.64928412896355,1.65143095725007,1.65278728562107,1.65385911841402,1.65510881737313,
1.65735083935026,1.66814601013867,1.69210638951572,1.74805404629795,1.75467929342998,
1.75721847962063,1.75904426635465,1.7609827183722,1.76355564981005,1.76921965307229,
1.79185993256202,1.82467490385176,1.82889898837517,1.86039111270683,1.8633024911439,
1.86469040503985,1.86576502144183,1.8669930726272,1.86913668712782,1.87844828159124,
1.92759392663568,1.96295408368725,1.96725123097806,1.96979276014188,1.97173318561002,
1.97380572632607,1.97705214516539,1.98734692570109,2.00387637583337,2.03673241895726,
2.04842499823039,2.05688773826077,2.0727339348878,2.07534613190607,2.07669163343502,
2.07776257369036,2.07902011570333,2.08129869010328,2.09271990509077,2.11908202301188,
2.17148524379948,2.17841603878784,2.1812881475847,2.1830817267577,2.18504165356763,
2.18774274371944,2.19413398865415,2.24049020802426,2.28167191070143,2.28635355340294,
2.28808858751266,2.28911271836411,2.29020548502977,2.29171944475299,2.2953247129901,
2.33382364959093,2.38313324211796,2.39030045978694,2.39321196698077,2.39501279634959,
2.39696692214965,2.39963523349187,2.40564810022727,2.41389768596798,2.46455540520303,
2.49625376527554,2.49916486350826,2.50055269798735,2.50162727784137,2.50285531516211,
2.50414746183214,2.50879710771578,2.53292412726831,2.55382470693563,2.59313914980931),
 .UNSPECIFIED.);
#1918=B_SPLINE_CURVE_WITH_KNOTS('',3,(#186024,#186025,#186026,#186027,#186028,
#186029,#186030,#186031,#186032,#186033,#186034,#186035,#186036,#186037,
#186038,#186039,#186040,#186041,#186042,#186043,#186044,#186045,#186046,
#186047,#186048,#186049,#186050,#186051,#186052,#186053,#186054,#186055,
#186056,#186057,#186058,#186059,#186060,#186061,#186062,#186063,#186064,
#186065,#186066,#186067,#186068,#186069,#186070,#186071,#186072,#186073,
#186074,#186075,#186076,#186077,#186078,#186079,#186080,#186081,#186082,
#186083,#186084,#186085,#186086,#186087,#186088,#186089,#186090,#186091,
#186092,#186093,#186094,#186095,#186096,#186097,#186098,#186099,#186100,
#186101,#186102,#186103,#186104,#186105,#186106,#186107,#186108,#186109,
#186110,#186111,#186112,#186113,#186114,#186115,#186116,#186117,#186118,
#186119,#186120,#186121,#186122,#186123,#186124,#186125,#186126,#186127,
#186128,#186129,#186130,#186131,#186132,#186133,#186134,#186135,#186136,
#186137,#186138,#186139,#186140,#186141,#186142,#186143,#186144,#186145,
#186146,#186147,#186148,#186149,#186150,#186151,#186152,#186153,#186154,
#186155,#186156,#186157,#186158,#186159,#186160,#186161,#186162,#186163,
#186164,#186165,#186166,#186167,#186168,#186169,#186170,#186171,#186172,
#186173,#186174,#186175,#186176,#186177,#186178,#186179,#186180,#186181,
#186182,#186183,#186184,#186185,#186186,#186187,#186188,#186189,#186190,
#186191,#186192,#186193,#186194,#186195,#186196,#186197,#186198,#186199,
#186200,#186201,#186202,#186203,#186204,#186205,#186206,#186207,#186208,
#186209,#186210,#186211,#186212,#186213,#186214,#186215,#186216,#186217,
#186218,#186219,#186220,#186221,#186222,#186223,#186224,#186225,#186226,
#186227,#186228,#186229,#186230,#186231,#186232,#186233,#186234,#186235,
#186236,#186237,#186238,#186239,#186240,#186241,#186242,#186243,#186244,
#186245,#186246,#186247,#186248,#186249,#186250,#186251,#186252,#186253,
#186254,#186255,#186256,#186257,#186258,#186259,#186260,#186261),
 .UNSPECIFIED.,.F.,.F.,(4,2,2,2,2,2,2,2,2,2,2,2,2,2,2,2,2,2,2,2,2,2,2,2,
2,2,2,2,2,2,2,2,2,2,2,2,2,2,2,2,2,2,2,2,2,2,2,2,2,2,2,2,2,2,2,2,2,2,2,2,
2,2,2,2,2,2,2,2,2,2,2,2,2,2,2,2,2,2,2,2,2,2,2,2,2,2,2,2,2,2,2,2,2,2,2,2,
2,2,2,2,2,2,2,2,2,2,2,2,2,2,2,2,2,2,2,2,2,2,4),(0.0750717851778821,0.0891453783474772,
0.1087192970361,0.112670157112163,0.114241193640968,0.115344696903057,0.116355376301621,
0.118019908363095,0.122250352987691,0.171173402583166,0.20895082471958,
0.213968579861932,0.216896951969535,0.219516741369516,0.221437752967846,
0.223232180483361,0.226106804357264,0.233033251402772,0.285519572440992,
0.311872492728247,0.323292252604327,0.325571279362092,0.326829154986186,
0.327900433628379,0.329246423208051,0.331859753701603,0.347731566056851,
0.352570265379959,0.367740061051498,0.400617568765758,0.417199257124334,
0.427519584284733,0.430769576126748,0.432843327658458,0.434784135670115,
0.437325083531694,0.441618854436347,0.476149367615986,0.496363447435444,
0.52357755700517,0.535211386266633,0.537502463284449,0.538762965732314,
0.539834057535949,0.541176739628813,0.54377468713262,0.559269099536909,
0.563494995426891,0.611468218857118,0.635181638865882,0.640989895303778,
0.643589461135923,0.645532474861167,0.647351300977577,0.649862938640005,
0.656315216532433,0.713883148579057,0.736844180074091,0.747364976192785,
0.749590459351435,0.750836730097221,0.751909224889602,0.753271024874312,
0.755957860227891,0.773745509226652,0.821985607898747,0.840287695048908,
0.851368557299992,0.854703013833243,0.856795400351583,0.858729449641452,
0.861227337197682,0.86537338167352,0.893311548684437,0.947028169980716,
0.959232734448808,0.961554775631366,0.962822073493619,0.963892853517728,
0.965227484351787,0.967302745495934,0.97725674140125,0.982892865066459,
0.992293088897469,1.00386246051483,1.0367091579207,1.05325022119457,1.06355259515346,
1.0668008364901,1.06887440950704,1.07081570981274,1.07335825373397,1.07765685492899,
1.11296692312606,1.16222109021709,1.17155869396154,1.17370493824424,1.17493394549453,
1.17600904522414,1.17739710677164,1.18030713251461,1.20843832112002,1.24812717812997,
1.26507257095043,1.27555724716827,1.27882646295807,1.2809047622708,1.28284443417117,
1.28537615186896,1.28963706461134,1.33463676212147,1.3796876555644,1.38441284821034,
1.38615514539917,1.38718113692288,1.38827383174263,1.38978433755491,1.39336594278135,
1.40879227668569),.UNSPECIFIED.);
#1919=B_SPLINE_CURVE_WITH_KNOTS('',3,(#186267,#186268,#186269,#186270,#186271),
 .UNSPECIFIED.,.F.,.F.,(4,1,4),(76.7075601022117,76.9104066470643,77.0584303621713),
 .UNSPECIFIED.);
#1920=B_SPLINE_CURVE_WITH_KNOTS('',3,(#186272,#186273,#186274,#186275,#186276,
#186277,#186278,#186279,#186280,#186281,#186282,#186283,#186284,#186285,
#186286,#186287,#186288,#186289,#186290,#186291,#186292,#186293,#186294,
#186295,#186296,#186297,#186298,#186299,#186300,#186301,#186302,#186303,
#186304,#186305,#186306,#186307,#186308,#186309,#186310,#186311,#186312,
#186313,#186314,#186315,#186316,#186317,#186318,#186319,#186320,#186321,
#186322,#186323,#186324,#186325,#186326,#186327,#186328,#186329,#186330,
#186331,#186332,#186333,#186334,#186335,#186336,#186337,#186338,#186339,
#186340,#186341,#186342,#186343,#186344,#186345,#186346,#186347,#186348,
#186349,#186350,#186351,#186352,#186353,#186354,#186355,#186356,#186357,
#186358,#186359,#186360,#186361,#186362,#186363,#186364,#186365,#186366,
#186367,#186368,#186369,#186370,#186371,#186372,#186373,#186374,#186375,
#186376,#186377,#186378,#186379,#186380,#186381,#186382,#186383,#186384,
#186385,#186386,#186387,#186388,#186389,#186390,#186391,#186392,#186393,
#186394,#186395,#186396,#186397,#186398,#186399,#186400,#186401,#186402,
#186403,#186404,#186405,#186406,#186407,#186408,#186409,#186410,#186411,
#186412,#186413,#186414,#186415,#186416,#186417,#186418,#186419,#186420,
#186421,#186422,#186423,#186424,#186425,#186426,#186427,#186428,#186429,
#186430,#186431,#186432,#186433,#186434,#186435,#186436,#186437,#186438,
#186439,#186440,#186441,#186442,#186443,#186444,#186445,#186446,#186447,
#186448,#186449,#186450,#186451,#186452,#186453,#186454,#186455,#186456,
#186457,#186458,#186459,#186460,#186461,#186462,#186463,#186464,#186465,
#186466,#186467,#186468,#186469,#186470,#186471,#186472,#186473,#186474,
#186475,#186476,#186477,#186478,#186479,#186480,#186481,#186482,#186483,
#186484,#186485,#186486,#186487,#186488,#186489,#186490,#186491,#186492,
#186493),.UNSPECIFIED.,.F.,.F.,(4,2,2,2,2,2,2,2,2,2,2,2,2,2,2,2,2,2,2,2,
2,2,2,2,2,2,2,2,2,2,2,2,2,2,2,2,2,2,2,2,2,2,2,2,2,2,2,2,2,2,2,2,2,2,2,2,
2,2,2,2,2,2,2,2,2,2,2,2,2,2,2,2,2,2,2,2,2,2,2,2,2,2,2,2,2,2,2,2,2,2,2,2,
2,2,2,2,2,2,2,2,2,2,2,2,2,2,2,2,2,2,4),(0.000629224533727324,0.0464126621687836,
0.0539626763531269,0.0578723762427416,0.0612145520135249,0.0633082415157978,
0.0652410855766748,0.0677340423634502,0.0718645896666564,0.0992472355725051,
0.113709321813746,0.129240598463086,0.154594556929824,0.16574178214956,
0.168010450595375,0.169268035226069,0.170339020864305,0.171684584897561,
0.174296920953314,0.190152334184,0.195974171156568,0.252803526465609,0.268941988849295,
0.272736140704197,0.27492968962085,0.276842832163743,0.279203717020773,
0.282811030182719,0.299535151121957,0.307018560652277,0.355524549263055,
0.370248675243035,0.378140658615438,0.380172201927849,0.381375365209586,
0.382455172270495,0.383862177879522,0.386228863793868,0.401659062722206,
0.405923222942093,0.448896318633739,0.476827918475772,0.483168208250224,
0.485860736611321,0.487819214716071,0.489614769057079,0.492497261265996,
0.499490239454971,0.551009931245716,0.578034136333571,0.589619962056034,
0.591907936138278,0.593167565483171,0.594238417515275,0.595581435666222,
0.598181887162465,0.61374689460685,0.620206441122678,0.661616806330857,
0.688886522740687,0.695146366432909,0.697825195494852,0.699781299801176,
0.701579962533769,0.704479107892417,0.711571657377543,0.76122499734123,
0.799535458073044,0.803139547680463,0.804653404254384,0.805746239795849,
0.806770550084666,0.808506131278771,0.813190663793015,0.854270227369256,
0.90069632129006,0.907087781284192,0.909789116784305,0.91174928044377,0.913543120827663,
0.916415733282814,0.923348165275279,0.975791238592437,1.00216327878638,
1.01358701357392,1.01586598151391,1.01712371118841,1.0181947968606,1.01954045672254,
1.02215289135757,1.03800315140485,1.04274645700524,1.05802368065071,1.09089683261881,
1.10747729817755,1.11779657959663,1.12104609091117,1.12311949953335,1.12505996113583,
1.12760041872033,1.13189327881161,1.17429056279923,1.20334593464797,1.22296047210307,
1.22691537197947,1.22848693012366,1.22959043091726,1.23060082410116,1.23226432129821,
1.23648912489059,1.25981860719964),.UNSPECIFIED.);
#1921=B_SPLINE_CURVE_WITH_KNOTS('',3,(#186495,#186496,#186497,#186498,#186499,
#186500,#186501,#186502,#186503,#186504,#186505,#186506,#186507,#186508,
#186509,#186510,#186511,#186512,#186513,#186514,#186515,#186516,#186517,
#186518,#186519,#186520,#186521,#186522,#186523,#186524,#186525,#186526,
#186527,#186528,#186529,#186530,#186531,#186532,#186533,#186534,#186535,
#186536,#186537,#186538,#186539,#186540,#186541,#186542,#186543,#186544,
#186545,#186546,#186547,#186548,#186549,#186550,#186551,#186552,#186553,
#186554,#186555,#186556,#186557,#186558,#186559,#186560,#186561,#186562,
#186563,#186564,#186565,#186566,#186567,#186568,#186569,#186570,#186571,
#186572,#186573,#186574,#186575,#186576,#186577,#186578,#186579,#186580,
#186581,#186582,#186583,#186584,#186585,#186586,#186587,#186588,#186589,
#186590,#186591,#186592,#186593,#186594,#186595,#186596,#186597,#186598,
#186599,#186600,#186601,#186602,#186603,#186604,#186605,#186606,#186607,
#186608,#186609,#186610,#186611,#186612,#186613,#186614,#186615,#186616,
#186617,#186618,#186619,#186620,#186621,#186622,#186623,#186624,#186625,
#186626,#186627,#186628,#186629,#186630,#186631,#186632,#186633,#186634,
#186635,#186636,#186637,#186638,#186639,#186640,#186641,#186642,#186643,
#186644,#186645,#186646,#186647,#186648,#186649,#186650,#186651,#186652,
#186653,#186654,#186655,#186656,#186657,#186658,#186659,#186660,#186661,
#186662,#186663,#186664,#186665,#186666,#186667,#186668,#186669,#186670,
#186671,#186672,#186673,#186674,#186675,#186676,#186677,#186678,#186679,
#186680,#186681,#186682,#186683,#186684,#186685,#186686,#186687,#186688,
#186689,#186690,#186691,#186692,#186693,#186694,#186695,#186696,#186697,
#186698,#186699,#186700,#186701,#186702,#186703,#186704,#186705,#186706,
#186707,#186708,#186709,#186710,#186711,#186712,#186713,#186714,#186715,
#186716,#186717,#186718),.UNSPECIFIED.,.F.,.F.,(4,2,2,2,2,2,2,2,2,2,2,2,
2,2,2,2,2,2,2,2,2,2,2,2,2,2,2,2,2,2,2,2,2,2,2,2,2,2,2,2,2,2,2,2,2,2,2,2,
2,2,2,2,2,2,2,2,2,2,2,2,2,2,2,2,2,2,2,2,2,2,2,2,2,2,2,2,2,2,2,2,2,2,2,2,
2,2,2,2,2,2,2,2,2,2,2,2,2,2,2,2,2,2,2,2,2,2,2,2,2,2,2,4),(1.40879227668569,
1.43100334476945,1.48142611167368,1.48848461841809,1.49137902606764,1.49317751608561,
1.49513563473351,1.4978212006631,1.50411510510166,1.53165386473917,1.56005743142361,
1.58238723262586,1.59509407049765,1.59733461345269,1.59871964715131,1.59979445276563,
1.60102543356578,1.603180548043,1.61264210716678,1.66182711478029,1.69703164539968,
1.70132887834435,1.70387110819822,1.70581244291945,1.7078863176153,1.71113558332165,
1.72144576985247,1.73800602081766,1.77089764691296,1.78463226584746,1.79150542719729,
1.79172194163246,1.79524178403218,1.80720044609824,1.80940049805829,1.81077325936907,
1.8118468169668,1.81308573798261,1.8152772015073,1.82526903226868,1.87400032445147,
1.90905752288329,1.91335254868163,1.91589404744955,1.91783515488805,1.9199091077548,
1.92315916620381,1.93347751982231,1.9500562679024,1.98296192190686,1.99814136604356,
2.00298749678178,2.01887889737035,2.02149317854504,2.02283948348095,2.02391092077113,
2.02516888112824,2.02744779212173,2.03886194855498,2.06518741968749,2.11768264226043,
2.12461220076899,2.12748488900246,2.12927914863838,2.1312400744361,2.13394300838327,
2.140340814811,2.18822154798705,2.2278321977224,2.23257803305534,2.23432327224965,
2.23534971398744,2.23644180490625,2.23794971234211,2.24151709177331,2.27899770614475,
2.32959370074135,2.33664136625753,2.33953364673658,2.34133151027224,2.34328949940916,
2.34597588921557,2.35227635373791,2.37987345685712,2.42202986271522,2.44273030124236,
2.44553853536011,2.44690652672951,2.44794318828084,2.44914403808312,2.45042586068833,
2.45237854022586,2.45600562423696,2.46464620226109,2.49771078806596,2.54136333775339,
2.54858725821568,2.55150906913563,2.55331236936547,2.55526611108923,2.55792840599244,
2.56408926771024,2.59055298369589,2.6480782413717,2.655950306731,2.65804641507783,
2.65927645566117,2.66033332044916,2.66137927037716,2.66272977103268,2.66518795266621,
2.66828177691447),.UNSPECIFIED.);
#1922=B_SPLINE_CURVE_WITH_KNOTS('',3,(#186719,#186720,#186721,#186722,#186723,
#186724),.UNSPECIFIED.,.F.,.F.,(4,2,4),(0.000817337931816071,0.0612279287495663,
0.0752219443712125),.UNSPECIFIED.);
#1923=B_SPLINE_CURVE_WITH_KNOTS('',3,(#186730,#186731,#186732,#186733,#186734,
#186735,#186736,#186737,#186738,#186739,#186740,#186741,#186742),
 .UNSPECIFIED.,.F.,.F.,(4,3,3,3,4),(82.9907456874214,83.0928761472026,83.194883423972,
83.2967928188117,83.3413404136697),.UNSPECIFIED.);
#1924=B_SPLINE_CURVE_WITH_KNOTS('',3,(#186743,#186744,#186745,#186746,#186747,
#186748,#186749,#186750,#186751,#186752),.UNSPECIFIED.,.F.,.F.,(4,1,1,1,
1,1,1,4),(77.0584303621713,77.9092430970262,78.9080795469881,79.9069159969499,
80.9057524469118,81.9045888968737,82.9034253468355,82.9907454093913),
 .UNSPECIFIED.);
#1925=B_SPLINE_CURVE_WITH_KNOTS('',3,(#186753,#186754,#186755,#186756,#186757,
#186758,#186759,#186760,#186761,#186762,#186763,#186764,#186765,#186766,
#186767,#186768,#186769,#186770,#186771,#186772,#186773,#186774,#186775,
#186776,#186777,#186778,#186779,#186780,#186781,#186782,#186783,#186784,
#186785,#186786,#186787,#186788,#186789,#186790,#186791,#186792,#186793,
#186794,#186795,#186796,#186797,#186798,#186799,#186800,#186801,#186802,
#186803,#186804,#186805,#186806,#186807,#186808,#186809,#186810,#186811,
#186812,#186813,#186814,#186815,#186816,#186817,#186818,#186819,#186820,
#186821,#186822,#186823,#186824,#186825,#186826,#186827,#186828,#186829,
#186830,#186831,#186832,#186833,#186834,#186835,#186836,#186837,#186838,
#186839,#186840,#186841,#186842,#186843,#186844,#186845,#186846,#186847,
#186848,#186849,#186850,#186851,#186852,#186853,#186854,#186855,#186856,
#186857,#186858,#186859,#186860,#186861,#186862,#186863,#186864,#186865,
#186866,#186867,#186868,#186869,#186870,#186871,#186872,#186873,#186874,
#186875,#186876,#186877,#186878,#186879,#186880,#186881,#186882,#186883,
#186884,#186885,#186886,#186887,#186888,#186889,#186890,#186891,#186892,
#186893,#186894,#186895,#186896,#186897,#186898,#186899,#186900,#186901,
#186902,#186903,#186904,#186905,#186906,#186907,#186908,#186909,#186910,
#186911,#186912,#186913,#186914,#186915,#186916,#186917,#186918,#186919,
#186920,#186921,#186922,#186923,#186924,#186925,#186926,#186927,#186928,
#186929,#186930,#186931,#186932,#186933,#186934,#186935,#186936,#186937,
#186938,#186939,#186940,#186941,#186942,#186943,#186944,#186945,#186946,
#186947,#186948,#186949,#186950,#186951,#186952,#186953,#186954,#186955,
#186956,#186957,#186958,#186959,#186960,#186961,#186962,#186963,#186964,
#186965,#186966,#186967,#186968,#186969,#186970,#186971,#186972,#186973,
#186974,#186975,#186976,#186977,#186978,#186979,#186980,#186981,#186982,
#186983,#186984,#186985,#186986,#186987,#186988,#186989,#186990,#186991,
#186992,#186993,#186994,#186995,#186996,#186997,#186998,#186999,#187000,
#187001,#187002,#187003,#187004,#187005,#187006,#187007,#187008,#187009,
#187010,#187011,#187012,#187013,#187014,#187015,#187016,#187017,#187018,
#187019,#187020,#187021,#187022,#187023,#187024,#187025,#187026,#187027,
#187028,#187029,#187030,#187031,#187032,#187033,#187034,#187035,#187036,
#187037,#187038,#187039,#187040,#187041,#187042,#187043,#187044,#187045,
#187046,#187047,#187048),.UNSPECIFIED.,.F.,.F.,(4,2,2,2,2,2,2,2,2,2,2,2,
2,2,2,2,2,2,2,2,2,2,2,2,2,2,2,2,2,2,2,2,2,2,2,2,2,2,2,2,2,2,2,2,2,2,2,2,
2,2,2,2,2,2,2,2,2,2,2,2,2,2,2,2,2,2,2,2,2,2,2,2,2,2,2,2,2,2,2,2,2,2,2,2,
2,2,2,2,2,2,2,2,2,2,2,2,2,2,2,2,2,2,2,2,2,2,2,2,2,2,2,2,2,2,2,2,2,2,2,2,
2,2,2,2,2,2,2,2,2,2,2,2,2,2,2,2,2,2,2,2,2,2,2,2,2,2,2,4),(0.0752219443712125,
0.0876741589246509,0.0938319992011081,0.0964930602826022,0.0984459259287984,
0.100248442114753,0.103169025493228,0.110390158188158,0.154176294194007,
0.195389487801746,0.199210492316058,0.201236328242508,0.202548271249196,
0.203772196473567,0.203775760638908,0.203779337406272,0.203782926793875,
0.203786752196306,0.203790639193609,0.203794588949303,0.203798602988633,
0.203802682582228,0.203806828968806,0.203811043788491,0.203815328656416,
0.203819685085049,0.203824114634023,0.203828618842948,0.20383319940526,
0.203837858157001,0.203842596887828,0.203847417344461,0.203852321440246,
0.203857311144556,0.203862388531956,0.203867555672481,0.203872814614456,
0.203878167614088,0.203883616968383,0.203889165102637,0.20389481435452,
0.203900567237911,0.204946646809773,0.20633648647122,0.208644419526527,
0.222699790354313,0.225486226583975,0.260904545343977,0.288832623753712,
0.303595725234263,0.307269947312214,0.30943720552109,0.311353669210471,
0.313753136775027,0.31748505469894,0.336116257030104,0.38037337776533,0.402096069778575,
0.412263463198908,0.414465903275958,0.415706920918454,0.416779704806643,
0.418148105791884,0.420959801995392,0.44205134961489,0.488505393083269,
0.512080552203394,0.517869970015435,0.520465800509764,0.522407891886507,
0.524227210683245,0.526741675709619,0.53321302692565,0.590596699260725,
0.61366136024826,0.624210159324676,0.626437064200589,0.627683484682615,
0.628755706021515,0.630116640354069,0.632800196507584,0.650505405323888,
0.698831972572652,0.717121417331737,0.728196142673682,0.73152948505618,
0.733621337627878,0.735555006061041,0.738052559850852,0.742198393831729,
0.770156025124721,0.823837018238989,0.836036730997686,0.838358160751868,
0.839625163885281,0.840695717955886,0.842030096170982,0.844105016945603,
0.85405834330488,0.859539959206553,0.85998801824992,0.866875720218246,0.88060109322453,
0.91346023515796,0.930021201358598,0.94033198236359,0.943580750552406,0.945654149542356,
0.947594928402469,0.950136272042241,0.954431684263708,0.989556857113646,
1.03848555421248,1.04826059725288,1.05043720290348,1.05167273380006,1.05274655787461,
1.05412383587971,1.05697955512463,1.07976013037356,1.09260331190984,1.12545738352177,
1.14200978542588,1.15231699138319,1.15556556846554,1.15763907029967,1.15958010336284,
1.16212200777224,1.16641887870625,1.20162447618504,1.25080410079112,1.26029292673091,
1.26244980068617,1.26368107044931,1.26475566998545,1.26613982522458,1.26903023718907,
1.29473233270021,1.33417764185622,1.3619000757016,1.36604053272241,1.36853691973143,
1.37047090166261,1.37256430523393,1.37590273724581,1.38701853300503,1.40540343092708,
1.40862562901102),.UNSPECIFIED.);
#1926=B_SPLINE_CURVE_WITH_KNOTS('',3,(#187054,#187055,#187056,#187057,#187058,
#187059,#187060,#187061,#187062,#187063,#187064,#187065,#187066,#187067,
#187068,#187069,#187070,#187071,#187072,#187073,#187074,#187075,#187076,
#187077,#187078,#187079),.UNSPECIFIED.,.F.,.F.,(4,2,2,2,2,2,2,2,2,2,2,2,
4),(2.59396462623471,2.61326336975643,2.62537967530848,2.62720696852797,
2.62820845138943,2.63689624976139,2.64004737281275,2.64189441921288,2.64374937154851,
2.64561742100235,2.64801886758359,2.65175877907383,2.66839194337532),
 .UNSPECIFIED.);
#1927=B_SPLINE_CURVE_WITH_KNOTS('',3,(#187080,#187081,#187082,#187083,#187084,
#187085,#187086,#187087,#187088,#187089,#187090,#187091,#187092,#187093,
#187094,#187095,#187096,#187097,#187098,#187099,#187100,#187101,#187102,
#187103,#187104,#187105,#187106,#187107,#187108,#187109,#187110,#187111,
#187112,#187113,#187114,#187115,#187116,#187117,#187118,#187119,#187120,
#187121,#187122,#187123,#187124,#187125,#187126,#187127,#187128,#187129,
#187130,#187131,#187132,#187133,#187134,#187135,#187136,#187137,#187138,
#187139,#187140,#187141,#187142,#187143,#187144,#187145,#187146,#187147,
#187148,#187149,#187150,#187151,#187152,#187153,#187154,#187155,#187156,
#187157,#187158,#187159,#187160,#187161,#187162,#187163,#187164,#187165,
#187166,#187167,#187168,#187169,#187170,#187171,#187172,#187173,#187174,
#187175,#187176,#187177,#187178,#187179,#187180,#187181,#187182,#187183,
#187184,#187185,#187186,#187187,#187188,#187189,#187190,#187191,#187192,
#187193,#187194,#187195,#187196,#187197,#187198,#187199,#187200,#187201,
#187202,#187203,#187204,#187205,#187206,#187207,#187208,#187209,#187210,
#187211,#187212,#187213,#187214,#187215,#187216,#187217,#187218,#187219,
#187220,#187221,#187222,#187223,#187224,#187225,#187226,#187227,#187228,
#187229,#187230,#187231,#187232,#187233,#187234,#187235,#187236,#187237,
#187238,#187239,#187240,#187241,#187242,#187243,#187244,#187245,#187246,
#187247,#187248,#187249,#187250,#187251,#187252,#187253,#187254,#187255,
#187256,#187257,#187258,#187259,#187260),.UNSPECIFIED.,.F.,.F.,(4,3,3,3,
3,3,3,3,3,3,3,3,3,3,3,3,3,3,3,3,3,3,3,3,3,3,3,3,3,3,3,3,3,3,3,3,3,3,3,3,
3,3,3,3,3,3,3,3,3,3,3,3,3,3,3,3,3,3,3,3,4),(83.3413404136697,83.4431910990492,
83.5450419838146,83.6469948549843,83.749004646587,83.8511877914694,83.9022617967974,
84.0056565338453,84.1088978159602,84.2120177813525,84.3150723495614,84.4180955579192,
84.5211214005918,84.6242541673699,84.7274432587797,84.8308152521614,84.9010982467593,
85.0044929838073,85.1077342659222,85.2108542313146,85.3139087995235,85.4169320078814,
85.5199578505541,85.6230906173322,85.726279708742,85.8296517021237,85.8999346967212,
86.0033294337691,86.1065707158841,86.2096906812763,86.3127452494852,86.4157684578429,
86.5187943005153,86.6219270672933,86.725116158703,86.8284881520847,86.898771146683,
87.0021658837309,87.1054071658459,87.2085271312383,87.3115816994472,87.4146049078051,
87.5176307504777,87.6207635172557,87.7239526086656,87.8273246020472,87.8976075966449,
88.0010023336927,88.1042436158081,88.2073635812004,88.3104181494092,88.4134413577669,
88.5164672004396,88.6195999672179,88.7227890586277,88.8261610520094,88.8964440466068,
89.013226996161,89.1295586830716,89.2451399878319,89.2739307161836),
 .UNSPECIFIED.);
#1928=B_SPLINE_CURVE_WITH_KNOTS('',3,(#187262,#187263,#187264,#187265,#187266,
#187267,#187268,#187269,#187270,#187271,#187272,#187273,#187274,#187275,
#187276,#187277,#187278,#187279,#187280,#187281,#187282,#187283,#187284,
#187285,#187286,#187287,#187288,#187289,#187290,#187291,#187292,#187293,
#187294,#187295,#187296,#187297,#187298,#187299,#187300,#187301,#187302,
#187303,#187304,#187305,#187306,#187307,#187308,#187309,#187310,#187311,
#187312,#187313,#187314,#187315,#187316,#187317,#187318,#187319,#187320,
#187321,#187322,#187323,#187324,#187325,#187326,#187327,#187328,#187329,
#187330,#187331,#187332,#187333,#187334,#187335,#187336,#187337,#187338,
#187339,#187340,#187341,#187342,#187343,#187344,#187345,#187346,#187347,
#187348,#187349,#187350,#187351,#187352,#187353,#187354,#187355,#187356,
#187357,#187358,#187359,#187360,#187361,#187362,#187363,#187364,#187365,
#187366,#187367,#187368,#187369,#187370,#187371,#187372,#187373,#187374,
#187375,#187376,#187377,#187378,#187379,#187380,#187381,#187382,#187383,
#187384,#187385,#187386,#187387,#187388,#187389,#187390,#187391,#187392,
#187393,#187394,#187395,#187396,#187397,#187398,#187399,#187400,#187401,
#187402,#187403,#187404,#187405,#187406,#187407,#187408,#187409,#187410,
#187411,#187412,#187413,#187414,#187415,#187416,#187417,#187418,#187419,
#187420,#187421,#187422,#187423,#187424,#187425,#187426,#187427,#187428,
#187429,#187430,#187431,#187432,#187433,#187434,#187435,#187436,#187437,
#187438,#187439,#187440,#187441,#187442,#187443,#187444,#187445,#187446,
#187447,#187448,#187449,#187450,#187451,#187452,#187453,#187454,#187455,
#187456,#187457,#187458,#187459,#187460,#187461,#187462,#187463,#187464,
#187465,#187466,#187467,#187468,#187469,#187470,#187471,#187472,#187473,
#187474,#187475,#187476,#187477,#187478,#187479,#187480,#187481,#187482,
#187483,#187484,#187485,#187486,#187487,#187488,#187489,#187490,#187491,
#187492,#187493,#187494,#187495,#187496,#187497,#187498,#187499,#187500,
#187501,#187502,#187503,#187504,#187505,#187506,#187507,#187508,#187509,
#187510,#187511,#187512,#187513,#187514,#187515,#187516,#187517,#187518,
#187519,#187520,#187521,#187522,#187523),.UNSPECIFIED.,.F.,.F.,(4,2,2,2,
2,2,2,2,2,2,2,2,2,2,2,2,2,2,2,2,2,2,2,2,2,2,2,2,2,2,2,2,2,2,2,2,2,2,2,2,
2,2,2,2,2,2,2,2,2,2,2,2,2,2,2,2,2,2,2,2,2,2,2,2,2,2,2,2,2,2,2,2,2,2,2,2,
2,2,2,2,2,2,2,2,2,2,2,2,2,2,2,2,2,2,2,2,2,2,2,2,2,2,2,2,2,2,2,2,2,2,2,2,
2,2,2,2,2,2,2,2,2,2,2,2,2,2,2,2,2,2,4),(1.40862562901102,1.45275465334309,
1.47131667206135,1.47406295265149,1.47541864509015,1.4764907850887,1.47774177390752,
1.47998843675736,1.49085062078179,1.51505365069752,1.55568297615944,1.57463747693525,
1.5783919344153,1.58079885741186,1.58271672890813,1.58488073561894,1.58853766675947,
1.60307206654821,1.63032533179596,1.67876836451512,1.68478514663889,1.68670426430569,
1.68788277604679,1.68897140844695,1.69045822973662,1.6939032895456,1.72313346562477,
1.74570987834384,1.78562285200694,1.79036910634731,1.79279768191903,1.79471784950775,
1.79686871775279,1.80046581033984,1.81427971855126,1.86523494593173,1.89514137108093,
1.89805696143434,1.89944616672057,1.90052145330931,1.90174990168535,1.90389334615704,
1.91319086897048,1.93203874251219,1.97244588542559,1.98470982990822,1.99933013990606,
2.00312041203308,2.00533624404761,2.00724903495114,2.00958446798186,2.01403440309192,
2.04490939879905,2.09135879679525,2.10759225452143,2.11022186822737,2.11157166359224,
2.11264356663356,2.11389939757671,2.11616765925701,2.12738963437662,2.1529565248882,
2.20656388285264,2.21341078381916,2.2162702887456,2.21806246255446,2.22002606159702,
2.22274177776183,2.22921303650886,2.283454208799,2.31941439185054,2.32227322542457,
2.32365141102349,2.32472566011931,2.3259613694899,2.32813753333291,2.33789844169634,
2.3868339999351,2.42195761873526,2.42625780458589,2.42880105388566,2.43074274832793,
2.43079405246234,2.43083662180819,2.43087314323725,2.43090447337441,2.43093134891346,
2.43095440282948,2.4309741786094,2.43099713623213,2.43101930521496,2.43104071477006,
2.43106139240282,2.43108136458104,2.43110065676173,2.4311192934721,2.43113729830345,
2.431154693942,2.43117150224622,2.43118774422328,2.43120344010428,2.43121860935849,
2.43123326905954,2.43124743556367,2.43126112922914,2.43127436672901,2.43347744507451,
2.43737358079612,2.44215984439604,2.45216496583788,2.48140966241379,2.52925235737917,
2.53360373449368,2.53528822805322,2.53630295226307,2.5374036461747,2.5389585551921,
2.54280720810928,2.56141800128267,2.61332592834438,2.62544453509487,2.62727217388184,
2.62827386152683,2.63696330633214,2.64011502741922,2.64196242458428,2.64381772922041,
2.64568613360734,2.64808803658774,2.65182865902094,2.66846498743977),
 .UNSPECIFIED.);
#1929=B_SPLINE_CURVE_WITH_KNOTS('',3,(#187524,#187525,#187526,#187527,#187528,
#187529,#187530,#187531,#187532,#187533),.UNSPECIFIED.,.F.,.F.,(4,3,3,4),
(-85.8723818947888,-85.7556989608338,-85.6390734939892,-85.5224480271446),
 .UNSPECIFIED.);
#1930=B_SPLINE_CURVE_WITH_KNOTS('',3,(#187538,#187539,#187540,#187541,#187542,
#187543,#187544,#187545,#187546,#187547,#187548,#187549,#187550,#187551,
#187552,#187553,#187554,#187555,#187556,#187557,#187558,#187559,#187560,
#187561,#187562,#187563,#187564,#187565,#187566,#187567,#187568,#187569,
#187570,#187571,#187572,#187573,#187574,#187575,#187576,#187577,#187578,
#187579,#187580,#187581,#187582,#187583,#187584,#187585,#187586,#187587,
#187588,#187589,#187590,#187591,#187592,#187593,#187594,#187595,#187596,
#187597,#187598,#187599,#187600,#187601,#187602,#187603,#187604,#187605,
#187606,#187607,#187608,#187609,#187610,#187611,#187612,#187613,#187614,
#187615,#187616,#187617,#187618,#187619,#187620,#187621,#187622,#187623,
#187624,#187625,#187626,#187627,#187628,#187629,#187630,#187631,#187632,
#187633,#187634,#187635,#187636,#187637,#187638,#187639,#187640,#187641,
#187642,#187643,#187644,#187645,#187646,#187647,#187648,#187649,#187650,
#187651,#187652,#187653,#187654,#187655,#187656,#187657,#187658,#187659,
#187660,#187661,#187662,#187663,#187664,#187665,#187666,#187667,#187668,
#187669,#187670,#187671,#187672,#187673,#187674,#187675,#187676,#187677,
#187678,#187679,#187680,#187681,#187682,#187683,#187684,#187685,#187686,
#187687,#187688,#187689,#187690,#187691,#187692,#187693,#187694,#187695,
#187696,#187697,#187698,#187699,#187700,#187701,#187702,#187703,#187704,
#187705,#187706,#187707,#187708,#187709,#187710,#187711,#187712,#187713,
#187714,#187715,#187716,#187717,#187718,#187719,#187720,#187721,#187722,
#187723,#187724,#187725,#187726,#187727,#187728,#187729,#187730,#187731,
#187732,#187733,#187734,#187735,#187736,#187737,#187738,#187739,#187740,
#187741,#187742,#187743,#187744,#187745,#187746,#187747,#187748,#187749,
#187750,#187751,#187752,#187753,#187754,#187755,#187756,#187757,#187758,
#187759,#187760,#187761,#187762,#187763,#187764,#187765,#187766,#187767,
#187768,#187769,#187770,#187771,#187772,#187773,#187774,#187775,#187776,
#187777,#187778,#187779,#187780,#187781,#187782,#187783,#187784,#187785,
#187786,#187787,#187788,#187789,#187790,#187791,#187792,#187793,#187794,
#187795,#187796,#187797,#187798,#187799,#187800,#187801,#187802,#187803,
#187804,#187805,#187806,#187807),.UNSPECIFIED.,.F.,.F.,(4,2,2,2,2,2,2,2,
2,2,2,2,2,2,2,2,2,2,2,2,2,2,2,2,2,2,2,2,2,2,2,2,2,2,2,2,2,2,2,2,2,2,2,2,
2,2,2,2,2,2,2,2,2,2,2,2,2,2,2,2,2,2,2,2,2,2,2,2,2,2,2,2,2,2,2,2,2,2,2,2,
2,2,2,2,2,2,2,2,2,2,2,2,2,2,2,2,2,2,2,2,2,2,2,2,2,2,2,2,2,2,2,2,2,2,2,2,
2,2,2,2,2,2,2,2,2,2,2,2,2,2,2,2,2,2,4),(1.26011167467531,1.26036620110984,
1.26252309759977,1.26375438023324,1.26482899100896,1.26621316074654,1.26910360307005,
1.2948059918053,1.33425167466812,1.36197439259648,1.36611489261192,1.36861130563355,
1.370545307773,1.37263873327601,1.37597720039364,1.38709311436655,1.40547820955506,
1.45282977752233,1.47139210604318,1.47413841893173,1.47549412626162,1.47656627752368,
1.47781727890539,1.48006396287666,1.49092622141433,1.51512936044351,1.55575920931139,
1.57471396780341,1.57846846917351,1.58087541875538,1.58279331043829,1.58495733886781,
1.5886143041484,1.60314880564022,1.63040221068751,1.67884451695401,1.68486249706948,
1.68678177571617,1.68796033119809,1.68904896250635,1.69053572317125,1.6939803842591,
1.72945135535193,1.78246408786581,1.78935678807242,1.79222364275473,1.79401701111302,
1.79597917410697,1.79868786515744,1.80511844941566,1.83379302284758,1.88510089038917,
1.89612188860234,1.89826694383392,1.89962305806149,1.9006953264991,1.90194622919679,
1.90419214778577,1.915039386318,1.93918522414623,1.99489369855084,2.00154884603247,
2.0040934196725,2.00592116805771,2.00785994413729,2.01043031510689,2.01607650279299,
2.03857613371646,2.07130937252344,2.1074095970491,2.11026970295025,2.11164800382076,
2.1127221089369,2.11395738884392,2.11613216586542,2.12587645497241,2.17481666259083,
2.20996024630414,2.21424769056579,2.21678703264344,2.21872783628879,2.22080276870796,
2.22405708904639,2.23441203774115,2.25107160559055,2.28404496995142,2.30299084398414,
2.30503213119893,2.30689970820413,2.3199977489731,2.32225818933318,2.32364912620884,
2.32472444563532,2.32595147163909,2.32808902506277,2.33730875288676,2.35591434346865,
2.40015966834944,2.42257657244587,2.42652189651186,2.42898690292306,2.43091098599602,
2.43093283747588,2.43095158235253,2.43097432285093,2.4309962825178,2.431017490333,
2.43103797350346,2.43105775823301,2.43107686974478,2.43109533224338,2.43111316913073,
2.43113040285866,2.43114705501466,2.43116314644866,2.43117869716484,2.43119372642108,
2.43120825105012,2.43122228711152,2.43123585496406,2.43124897111116,2.43345298341257,
2.43735447449341,2.44214904098073,2.45217907199654,2.48154435456666,2.52915549901937,
2.53354229444586,2.53523233117229,2.5362479929801,2.53734757336637,2.53889734934271,
2.54271553111527,2.56104983964384,2.59396462623471),.UNSPECIFIED.);
#1931=B_SPLINE_CURVE_WITH_KNOTS('',3,(#187809,#187810,#187811,#187812,#187813,
#187814,#187815,#187816,#187817,#187818,#187819,#187820,#187821,#187822,
#187823,#187824,#187825,#187826,#187827,#187828,#187829,#187830,#187831,
#187832,#187833,#187834,#187835,#187836,#187837,#187838,#187839,#187840,
#187841,#187842,#187843,#187844,#187845,#187846,#187847,#187848,#187849,
#187850,#187851,#187852,#187853,#187854,#187855,#187856,#187857,#187858,
#187859,#187860,#187861,#187862,#187863,#187864,#187865,#187866,#187867,
#187868,#187869,#187870,#187871,#187872,#187873,#187874,#187875,#187876,
#187877,#187878,#187879,#187880,#187881,#187882,#187883,#187884,#187885,
#187886,#187887,#187888,#187889,#187890,#187891,#187892,#187893,#187894,
#187895,#187896,#187897,#187898,#187899,#187900,#187901,#187902,#187903,
#187904,#187905,#187906,#187907,#187908,#187909,#187910,#187911,#187912,
#187913,#187914,#187915,#187916,#187917,#187918,#187919,#187920,#187921,
#187922,#187923,#187924,#187925,#187926,#187927,#187928,#187929,#187930,
#187931,#187932,#187933,#187934,#187935,#187936,#187937,#187938,#187939,
#187940,#187941,#187942,#187943,#187944,#187945,#187946,#187947,#187948,
#187949,#187950,#187951,#187952,#187953,#187954,#187955,#187956,#187957,
#187958,#187959,#187960,#187961,#187962,#187963,#187964,#187965,#187966,
#187967,#187968,#187969,#187970,#187971,#187972,#187973,#187974,#187975,
#187976,#187977,#187978,#187979,#187980,#187981,#187982,#187983,#187984,
#187985,#187986,#187987,#187988,#187989),.UNSPECIFIED.,.F.,.F.,(4,3,3,3,
3,3,3,3,3,3,3,3,3,3,3,3,3,3,3,3,3,3,3,3,3,3,3,3,3,3,3,3,3,3,3,3,3,3,3,3,
3,3,3,3,3,3,3,3,3,3,3,3,3,3,3,3,3,3,3,3,4),(-91.8056330559226,-91.703478392047,
-91.6014794906872,-91.4995669524813,-91.397705213372,-91.2958587787104,
-91.193920770489,-91.0919397623291,-90.9897717066981,-90.8941169465305,
-90.7907222094827,-90.6874809273678,-90.5843609619755,-90.4813063937666,
-90.3782831854088,-90.2752573427364,-90.1721245759583,-90.0689354845486,
-89.965563491167,-89.8952804965687,-89.7918857595209,-89.6886444774056,
-89.5855245120134,-89.4824699438045,-89.3794467354468,-89.2764208927745,
-89.1732881259964,-89.0700990345866,-88.966727041205,-88.8964440466068,
-88.7930493095589,-88.6898080274438,-88.5866880620515,-88.4836334938425,
-88.3806102854848,-88.2775844428123,-88.1744516760343,-88.0712625846244,
-87.9678905912427,-87.8976075966449,-87.794212859597,-87.6909715774818,
-87.5878516120896,-87.4847970438808,-87.3817738355231,-87.2787479928507,
-87.1756152260725,-87.0724261346628,-86.9690541412812,-86.898771146683,
-86.7953764096352,-86.69213512752,-86.5890151621277,-86.4859605939188,-86.382937385561,
-86.2799115428887,-86.1767787761105,-86.0735896847008,-85.9702176913191,
-85.8999346967212,-85.8723818947888),.UNSPECIFIED.);
#1932=B_SPLINE_CURVE_WITH_KNOTS('',3,(#187990,#187991,#187992,#187993,#187994),
 .UNSPECIFIED.,.F.,.F.,(4,1,4),(-92.1566391646458,-91.8929533964924,-91.8056333339369),
 .UNSPECIFIED.);
#1933=B_SPLINE_CURVE_WITH_KNOTS('',3,(#188000,#188001,#188002,#188003,#188004,
#188005,#188006,#188007,#188008,#188009,#188010,#188011,#188012,#188013,
#188014,#188015,#188016,#188017,#188018,#188019,#188020,#188021),
 .UNSPECIFIED.,.F.,.F.,(4,2,2,2,2,2,2,2,2,2,4),(2.59434030580712,2.6245953507381,
2.6484152592862,2.65628687327347,2.65838285903235,2.65961282848372,2.66066963231726,
2.66171552239248,2.66306594609527,2.66552398461768,2.6686176292093),
 .UNSPECIFIED.);
#1934=B_SPLINE_CURVE_WITH_KNOTS('',3,(#188022,#188023,#188024,#188025,#188026,
#188027,#188028,#188029,#188030,#188031,#188032,#188033,#188034,#188035,
#188036,#188037,#188038,#188039,#188040,#188041,#188042,#188043,#188044,
#188045,#188046,#188047,#188048,#188049,#188050,#188051,#188052,#188053,
#188054,#188055,#188056,#188057,#188058,#188059,#188060,#188061,#188062,
#188063,#188064,#188065,#188066,#188067,#188068,#188069,#188070,#188071,
#188072,#188073,#188074,#188075,#188076,#188077,#188078,#188079,#188080,
#188081,#188082,#188083,#188084,#188085,#188086,#188087,#188088,#188089,
#188090,#188091,#188092,#188093,#188094,#188095,#188096,#188097,#188098,
#188099,#188100,#188101,#188102,#188103,#188104,#188105,#188106,#188107,
#188108,#188109,#188110,#188111,#188112,#188113,#188114,#188115,#188116,
#188117,#188118,#188119,#188120,#188121,#188122,#188123,#188124,#188125,
#188126,#188127,#188128,#188129,#188130,#188131,#188132,#188133,#188134,
#188135,#188136,#188137,#188138,#188139,#188140,#188141,#188142,#188143,
#188144,#188145,#188146,#188147,#188148,#188149,#188150,#188151,#188152,
#188153,#188154,#188155,#188156,#188157,#188158,#188159,#188160,#188161,
#188162,#188163,#188164,#188165,#188166,#188167,#188168,#188169,#188170,
#188171,#188172,#188173,#188174,#188175,#188176,#188177,#188178,#188179,
#188180,#188181,#188182,#188183,#188184,#188185,#188186,#188187,#188188,
#188189,#188190,#188191,#188192,#188193,#188194,#188195,#188196,#188197,
#188198,#188199,#188200,#188201,#188202,#188203,#188204,#188205,#188206,
#188207,#188208,#188209,#188210,#188211,#188212,#188213,#188214,#188215,
#188216,#188217,#188218,#188219,#188220,#188221,#188222,#188223,#188224,
#188225,#188226,#188227,#188228,#188229,#188230,#188231,#188232,#188233,
#188234,#188235,#188236,#188237,#188238,#188239,#188240,#188241,#188242,
#188243,#188244,#188245,#188246,#188247,#188248,#188249,#188250,#188251,
#188252,#188253,#188254,#188255,#188256,#188257,#188258,#188259,#188260,
#188261,#188262,#188263),.UNSPECIFIED.,.F.,.F.,(4,2,2,2,2,2,2,2,2,2,2,2,
2,2,2,2,2,2,2,2,2,2,2,2,2,2,2,2,2,2,2,2,2,2,2,2,2,2,2,2,2,2,2,2,2,2,2,2,
2,2,2,2,2,2,2,2,2,2,2,2,2,2,2,2,2,2,2,2,2,2,2,2,2,2,2,2,2,2,2,2,2,2,2,2,
2,2,2,2,2,2,2,2,2,2,2,2,2,2,2,2,2,2,2,2,2,2,2,2,2,2,2,2,2,2,2,2,2,2,2,2,
4),(0.000817344774108441,0.0612254651869213,0.0876737802003372,0.0938318808098746,
0.0964929874989253,0.0984458613996463,0.100248367484044,0.10316889486537,
0.110389693522579,0.154248043816412,0.195394654296778,0.199212997128793,
0.201237831272896,0.202549359042334,0.203772991306706,0.203776558034222,
0.203780137465953,0.203783729587056,0.203787567161818,0.203791466614978,
0.203795429174728,0.203799456164751,0.203803549140782,0.20380770937905,
0.203811938279478,0.203816237472464,0.203820608422661,0.203825052813434,
0.203829572297477,0.203834168460689,0.203838843215121,0.203843598289257,
0.203848435483984,0.204892224678134,0.206274994503329,0.209159894927432,
0.24333536368996,0.277585018344356,0.294134253468309,0.304439228580753,
0.307686964814489,0.309759896851876,0.311700373268492,0.314241515163701,
0.318537021927793,0.353721240095344,0.402848914196404,0.412378986999385,
0.414538347548047,0.415769950810159,0.416844139401268,0.418226843280678,
0.421111008852201,0.445864786342485,0.488791041320977,0.512159280939036,
0.517921466523687,0.520512484215026,0.52245393171994,0.524274797102512,
0.52679481126563,0.533299398727068,0.590405896585106,0.613651227045902,
0.624250482074529,0.626480659006351,0.627727855653289,0.628800088943574,
0.630160194117394,0.632319147710258,0.643575675048509,0.694430300562819,
0.723203038571217,0.729644822313636,0.732354887197064,0.73431683582354,
0.736109180619974,0.738972588319888,0.745847597131116,0.799079313312624,
0.814907809651494,0.835599169805093,0.83822332834501,0.839554065022661,
0.840614463375584,0.841880332663877,0.844133041559424,0.853786512644175,
0.859625398223345,0.860058972458099,0.866943612928567,0.880670433562754,
0.913529926085419,0.93009107766879,0.940401971870878,0.943650774638628,
0.945724195442819,0.94766499454514,0.950206364438463,0.954501820478792,
0.989627292276999,1.03855634677172,1.04833167342516,1.05050831422143,1.05174386075997,
1.05281769567492,1.05419498399687,1.05705071230623,1.07983069381489,1.09267484391548,
1.12552926030726,1.14208184059342,1.15238915658118,1.15563776787846,1.15771129144662,
1.15965234478391,1.16219427564375,1.16649119107448,1.20169713841453,1.25087727607578,
1.26011167467531),.UNSPECIFIED.);
#1935=B_SPLINE_CURVE_WITH_KNOTS('',3,(#188265,#188266,#188267,#188268,#188269,
#188270,#188271,#188272,#188273,#188274),.UNSPECIFIED.,.F.,.F.,(4,1,1,1,
1,1,1,4),(-98.0888186411165,-97.8859720962637,-96.8871356463018,-95.8882991963399,
-94.889462746378,-93.8906262964162,-92.8917898464543,-92.1566391646458),
 .UNSPECIFIED.);
#1936=B_SPLINE_CURVE_WITH_KNOTS('',3,(#188275,#188276,#188277,#188278,#188279,
#188280,#188281,#188282,#188283,#188284,#188285,#188286,#188287,#188288,
#188289,#188290,#188291,#188292,#188293,#188294),.UNSPECIFIED.,.F.,.F.,
(4,2,2,2,2,2,2,2,2,4),(0.000629226904789768,0.0468422160482133,0.0541658165813541,
0.0579911959946999,0.0612752724550681,0.0633561448110693,0.0652934439714124,
0.0678152483376244,0.0720443780039375,0.07510365538255),.UNSPECIFIED.);
#1937=B_SPLINE_CURVE_WITH_KNOTS('',3,(#188299,#188300,#188301,#188302,#188303,
#188304,#188305,#188306,#188307,#188308,#188309,#188310,#188311,#188312,
#188313,#188314,#188315,#188316,#188317,#188318,#188319,#188320,#188321,
#188322,#188323,#188324,#188325,#188326,#188327,#188328,#188329,#188330,
#188331,#188332,#188333,#188334,#188335,#188336,#188337,#188338,#188339,
#188340,#188341,#188342,#188343,#188344,#188345,#188346,#188347,#188348,
#188349,#188350,#188351,#188352,#188353,#188354,#188355,#188356,#188357,
#188358,#188359,#188360,#188361,#188362,#188363,#188364,#188365,#188366,
#188367,#188368,#188369,#188370,#188371,#188372,#188373,#188374,#188375,
#188376,#188377,#188378,#188379,#188380,#188381,#188382,#188383,#188384,
#188385,#188386,#188387,#188388,#188389,#188390,#188391,#188392,#188393,
#188394,#188395,#188396,#188397,#188398,#188399,#188400,#188401,#188402,
#188403,#188404,#188405,#188406,#188407,#188408,#188409,#188410,#188411,
#188412,#188413,#188414,#188415,#188416,#188417,#188418,#188419,#188420,
#188421,#188422,#188423,#188424,#188425,#188426,#188427,#188428,#188429,
#188430,#188431,#188432,#188433,#188434,#188435,#188436,#188437,#188438,
#188439,#188440,#188441,#188442,#188443,#188444,#188445,#188446,#188447,
#188448,#188449,#188450,#188451,#188452,#188453,#188454,#188455,#188456,
#188457,#188458,#188459,#188460,#188461,#188462,#188463,#188464,#188465,
#188466,#188467,#188468,#188469,#188470,#188471,#188472,#188473,#188474,
#188475,#188476,#188477,#188478,#188479,#188480,#188481,#188482,#188483,
#188484,#188485,#188486,#188487,#188488,#188489,#188490,#188491,#188492,
#188493,#188494,#188495,#188496,#188497,#188498,#188499,#188500,#188501,
#188502,#188503,#188504,#188505,#188506,#188507,#188508,#188509,#188510,
#188511,#188512,#188513,#188514,#188515,#188516,#188517,#188518,#188519,
#188520,#188521,#188522,#188523,#188524,#188525,#188526,#188527,#188528,
#188529,#188530,#188531,#188532,#188533,#188534,#188535,#188536),
 .UNSPECIFIED.,.F.,.F.,(4,2,2,2,2,2,2,2,2,2,2,2,2,2,2,2,2,2,2,2,2,2,2,2,
2,2,2,2,2,2,2,2,2,2,2,2,2,2,2,2,2,2,2,2,2,2,2,2,2,2,2,2,2,2,2,2,2,2,2,2,
2,2,2,2,2,2,2,2,2,2,2,2,2,2,2,2,2,2,2,2,2,2,2,2,2,2,2,2,2,2,2,2,2,2,2,2,
2,2,2,2,2,2,2,2,2,2,2,2,2,2,2,2,2,2,2,2,2,2,4),(1.26027877606838,1.26524564787062,
1.27573161663081,1.27900123511885,1.28107979036348,1.28301970107747,1.2855517304173,
1.289813167522,1.3348183954334,1.3798748277065,1.38460060111834,1.38634311267145,
1.38736923049169,1.38846205987685,1.38997275181412,1.39355479886493,1.43119698698182,
1.4816257776398,1.4886851614224,1.49157992677149,1.4933786384757,1.49533699802944,
1.49802289353801,1.50431756659891,1.53185966588531,1.56026675308619,1.58259932665336,
1.59530772341971,1.59754854193088,1.59893374606931,1.60000868401374,1.601239816457,
1.60339519662903,1.61285792564873,1.6620489837926,1.69725782955956,1.70155559116883,
1.70409813391085,1.70603970764331,1.708113837747,1.7113635037859,1.72167496212459,
1.7382372576002,1.77113293498692,1.78487000733137,1.79174219333639,1.79195138979034,
1.79528676880761,1.80742214727915,1.80963215745186,1.81100801789834,1.81208197721038,
1.8133190746358,1.81550181014409,1.82536090297181,1.8742096216054,1.90930927696582,
1.91360534002856,1.91614729827708,1.91808866777881,1.92016281446589,1.92341299668222,
1.9337302254574,1.95030572194142,1.98321101347395,1.99803204453847,2.00309193599487,
2.01913276619391,2.0217547938998,2.02310286376967,2.02417453564695,2.02543141545218,
2.0277049202389,2.03902099952282,2.06495714148558,2.11802004762081,2.12490878320021,
2.12777496727722,2.12956820019529,2.1315304434071,2.13423966414903,2.14067349122147,
2.16937555772329,2.22064733913027,2.23167081379126,2.23381600625513,2.23517215443313,
2.23624441445118,2.2374952667592,2.23974099354813,2.25058535783602,2.27472070108179,
2.33044405824917,2.33709758063341,2.3396418834895,2.34146954722493,2.3434083345115,
2.34597889199367,2.35162618747065,2.37413421066519,2.40687263517928,2.44295971787812,
2.44581771749361,2.44719559579556,2.44823499175961,2.44943036425619,2.45070437258797,
2.45263807730776,2.45621530280002,2.46468816980605,2.52438370686324,2.54621101977488,
2.55012782909812,2.55258417318313,2.55450718821749,2.55664152460183,2.56016490711316,
2.573150222639,2.59434030580712),.UNSPECIFIED.);
#1938=B_SPLINE_CURVE_WITH_KNOTS('',3,(#188537,#188538,#188539,#188540,#188541,
#188542,#188543,#188544,#188545,#188546,#188547,#188548,#188549,#188550,
#188551,#188552,#188553,#188554,#188555,#188556,#188557,#188558,#188559,
#188560,#188561,#188562,#188563,#188564,#188565,#188566,#188567,#188568,
#188569,#188570,#188571,#188572,#188573,#188574,#188575,#188576,#188577,
#188578,#188579,#188580,#188581,#188582,#188583,#188584,#188585,#188586,
#188587,#188588,#188589,#188590,#188591,#188592,#188593,#188594,#188595,
#188596,#188597,#188598,#188599,#188600,#188601,#188602,#188603,#188604,
#188605,#188606,#188607,#188608,#188609,#188610,#188611,#188612,#188613,
#188614,#188615,#188616,#188617,#188618,#188619,#188620,#188621,#188622,
#188623,#188624,#188625,#188626,#188627,#188628,#188629,#188630,#188631,
#188632,#188633,#188634,#188635,#188636,#188637,#188638,#188639,#188640,
#188641,#188642,#188643,#188644,#188645,#188646,#188647,#188648,#188649,
#188650,#188651,#188652,#188653,#188654,#188655,#188656,#188657,#188658,
#188659,#188660,#188661,#188662,#188663,#188664,#188665,#188666,#188667,
#188668,#188669,#188670,#188671,#188672,#188673,#188674,#188675,#188676,
#188677,#188678,#188679,#188680,#188681,#188682,#188683,#188684,#188685,
#188686,#188687,#188688,#188689,#188690,#188691,#188692,#188693,#188694,
#188695,#188696,#188697,#188698,#188699,#188700,#188701,#188702,#188703,
#188704,#188705,#188706,#188707,#188708,#188709,#188710,#188711,#188712,
#188713,#188714,#188715,#188716,#188717,#188718,#188719,#188720,#188721,
#188722,#188723,#188724,#188725,#188726,#188727,#188728,#188729,#188730,
#188731,#188732,#188733,#188734,#188735,#188736,#188737,#188738,#188739,
#188740,#188741,#188742,#188743,#188744,#188745,#188746,#188747,#188748,
#188749,#188750,#188751,#188752,#188753,#188754,#188755,#188756,#188757,
#188758),.UNSPECIFIED.,.F.,.F.,(4,2,2,2,2,2,2,2,2,2,2,2,2,2,2,2,2,2,2,2,
2,2,2,2,2,2,2,2,2,2,2,2,2,2,2,2,2,2,2,2,2,2,2,2,2,2,2,2,2,2,2,2,2,2,2,2,
2,2,2,2,2,2,2,2,2,2,2,2,2,2,2,2,2,2,2,2,2,2,2,2,2,2,2,2,2,2,2,2,2,2,2,2,
2,2,2,2,2,2,2,2,2,2,2,2,2,2,2,2,2,2,4),(0.07510365538255,0.118699139152014,
0.138790157978397,0.156962085014619,0.16602189526956,0.16806255948916,0.169315637659534,
0.170387061309427,0.17173863570937,0.174378777665775,0.190911462663399,
0.199764478504622,0.243740970988521,0.259906867840923,0.269996178958814,
0.27324363747737,0.275316468634537,0.277256904275559,0.279798070205302,
0.284093791180943,0.319303404930741,0.368518684618085,0.37794588264825,
0.380097921466115,0.381327889660885,0.382402299070527,0.383787453978794,
0.386029423626997,0.398777710807198,0.401649171323257,0.405936049248987,
0.448926926547703,0.476866462847058,0.48320809679262,0.485901063361633,
0.487859811477717,0.48965557961469,0.492538340964345,0.499531593624987,
0.551068240041451,0.57808859415,0.589674108944058,0.591962278701603,0.59322204955337,
0.594293042224718,0.595636262538031,0.598237180575012,0.613807233449575,
0.620261548200421,0.661679496467052,0.688953302732904,0.69521402633163,
0.697893214611427,0.699849574778535,0.701648468285654,0.704547975669279,
0.711641360810562,0.761303033561479,0.799616738266917,0.803221278945533,
0.804735329128075,0.805828305971827,0.806852749917557,0.808588560148625,
0.81327372579607,0.854357786507452,0.900790720169797,0.907183012256262,
0.909884698727915,0.911845116798863,0.913639189823246,0.916512174419259,
0.92344550237546,0.97589545436355,1.00227087738279,1.01369608503042,1.01597534814017,
1.01723324088855,1.01830446553677,1.01965030011911,1.02226307429011,1.03811541458428,
1.04285979830379,1.05813854118807,1.09101595881515,1.10759857242159,1.11791919142461,
1.12116912421312,1.12324280182285,1.12518351520449,1.12772430247277,1.13201771977366,
1.17442051842454,1.20347967363437,1.22309674950585,1.22705216189747,1.2286239238493,
1.22972756779993,1.23073809209405,1.23240180520209,1.23662715741319,1.28597339651562,
1.32674441864755,1.33181099193912,1.33427077596588,1.33619387704901,1.33832563687611,
1.3418385910895,1.35471538062677,1.37741913899921,1.40857222162858),
 .UNSPECIFIED.);
#1939=B_SPLINE_CURVE_WITH_KNOTS('',3,(#188764,#188765,#188766,#188767),
 .UNSPECIFIED.,.F.,.F.,(4,4),(114.406674973133,114.756144625377),
 .UNSPECIFIED.);
#1940=B_SPLINE_CURVE_WITH_KNOTS('',3,(#188768,#188769,#188770,#188771,#188772,
#188773,#188774,#188775,#188776,#188777,#188778,#188779,#188780,#188781,
#188782,#188783,#188784,#188785,#188786,#188787,#188788,#188789,#188790,
#188791,#188792,#188793,#188794,#188795,#188796,#188797,#188798,#188799,
#188800,#188801,#188802,#188803,#188804,#188805,#188806,#188807,#188808,
#188809,#188810,#188811,#188812,#188813,#188814,#188815,#188816,#188817,
#188818,#188819,#188820,#188821,#188822,#188823,#188824,#188825,#188826,
#188827,#188828,#188829,#188830,#188831,#188832,#188833,#188834,#188835,
#188836,#188837,#188838,#188839,#188840,#188841,#188842,#188843,#188844,
#188845,#188846,#188847,#188848,#188849,#188850,#188851,#188852,#188853,
#188854,#188855,#188856,#188857,#188858,#188859,#188860,#188861,#188862,
#188863,#188864,#188865,#188866,#188867,#188868,#188869,#188870,#188871,
#188872,#188873,#188874,#188875,#188876,#188877,#188878,#188879,#188880,
#188881,#188882,#188883,#188884,#188885,#188886,#188887,#188888,#188889,
#188890,#188891,#188892,#188893,#188894,#188895,#188896,#188897,#188898,
#188899,#188900,#188901,#188902,#188903,#188904,#188905,#188906,#188907,
#188908,#188909,#188910,#188911,#188912,#188913,#188914,#188915,#188916,
#188917,#188918,#188919,#188920,#188921,#188922,#188923,#188924,#188925,
#188926,#188927,#188928,#188929,#188930,#188931,#188932,#188933,#188934,
#188935,#188936,#188937,#188938,#188939,#188940,#188941,#188942,#188943,
#188944,#188945,#188946,#188947,#188948,#188949,#188950,#188951,#188952,
#188953,#188954,#188955,#188956,#188957,#188958,#188959,#188960,#188961,
#188962,#188963,#188964,#188965,#188966,#188967,#188968,#188969,#188970,
#188971,#188972,#188973,#188974,#188975,#188976,#188977,#188978,#188979,
#188980,#188981,#188982,#188983),.UNSPECIFIED.,.F.,.F.,(4,2,2,2,2,2,2,2,
2,2,2,2,2,2,2,2,2,2,2,2,2,2,2,2,2,2,2,2,2,2,2,2,2,2,2,2,2,2,2,2,2,2,2,2,
2,2,2,2,2,2,2,2,2,2,2,2,2,2,2,2,2,2,2,2,2,2,2,2,2,2,2,2,2,2,2,2,2,2,2,2,
2,2,2,2,2,2,2,2,2,2,2,2,2,2,2,2,2,2,2,2,2,2,2,2,2,2,2,4),(0.000658788637333733,
0.00332970111957805,0.00592165798483083,0.0077887962721166,0.00964368910378566,
0.0114909184364534,0.0146445377755957,0.0233614973535325,0.0917305383706879,
0.109072658587112,0.11278023260465,0.114311678894522,0.115407806628788,
0.116427795994408,0.118140544916847,0.122673808701606,0.169412955505319,
0.208756977489166,0.213872139697951,0.216839912671708,0.218921119844328,
0.220936314295769,0.222824215644402,0.225366501659542,0.229665126650277,
0.264781240463593,0.313699435168169,0.323487525706099,0.325665035363407,
0.326900771559257,0.327974577129087,0.329351574097245,0.332205826048581,
0.368431090342151,0.401082247997168,0.423502301778862,0.42913761828349,
0.431705733361184,0.433643908600663,0.435471904780948,0.438018132669157,
0.444685431694998,0.50028231196104,0.507358872502943,0.526258691274849,
0.535571224662673,0.537715472399808,0.538943942213686,0.540018966728738,
0.541407452178281,0.544320203781764,0.575418056595013,0.612230822589427,
0.635386119473837,0.641120659152872,0.643707074772631,0.645648217483469,
0.647471088553852,0.649997525125904,0.656539227443313,0.713347962515895,
0.73680029409589,0.747457798552966,0.749692019981419,0.750940309815345,
0.75201275803801,0.753372203310128,0.756047454830763,0.773495653696656,
0.823321313642927,0.840834961354449,0.85157199955984,0.854869286014235,
0.856953659334793,0.858890851091243,0.86140772925105,0.865618046493869,
0.896124831263709,0.94741967598083,0.959389844840715,0.96169968808587,0.962964446605137,
0.964035530772473,0.965373629313709,0.967459886864002,0.977570751556628,
0.983042494056251,0.992430706109514,1.00400338717725,1.0368541374581,1.05339725147272,
1.06370090016748,1.06694954215721,1.06902337064208,1.07096490991329,1.07350776651685,
1.07780689570321,1.11312122396326,1.1623815072661,1.1717202766068,1.17386678628622,
1.17509594511129,1.17617117717746,1.17755940925831,1.18046979137668,1.20860412800414,
1.24829816471492,1.26027877606838),.UNSPECIFIED.);
#1941=B_SPLINE_CURVE_WITH_KNOTS('',3,(#188985,#188986,#188987,#188988,#188989,
#188990,#188991,#188992,#188993,#188994,#188995,#188996,#188997,#188998,
#188999,#189000,#189001,#189002,#189003,#189004,#189005,#189006,#189007,
#189008,#189009,#189010,#189011,#189012,#189013,#189014,#189015,#189016,
#189017,#189018,#189019,#189020,#189021,#189022,#189023,#189024,#189025,
#189026,#189027,#189028,#189029,#189030,#189031,#189032,#189033,#189034,
#189035,#189036,#189037,#189038,#189039,#189040,#189041,#189042,#189043,
#189044,#189045,#189046,#189047,#189048,#189049,#189050,#189051,#189052,
#189053,#189054,#189055,#189056,#189057,#189058,#189059,#189060,#189061,
#189062,#189063,#189064,#189065,#189066,#189067,#189068,#189069,#189070,
#189071,#189072,#189073,#189074,#189075,#189076,#189077,#189078,#189079,
#189080,#189081,#189082,#189083,#189084,#189085,#189086,#189087,#189088,
#189089,#189090,#189091,#189092,#189093,#189094,#189095,#189096,#189097,
#189098,#189099,#189100,#189101,#189102,#189103,#189104,#189105,#189106,
#189107,#189108,#189109,#189110,#189111,#189112,#189113,#189114,#189115,
#189116,#189117,#189118,#189119,#189120,#189121,#189122,#189123,#189124,
#189125,#189126,#189127,#189128,#189129,#189130,#189131,#189132,#189133,
#189134,#189135,#189136,#189137,#189138,#189139,#189140,#189141,#189142,
#189143,#189144,#189145,#189146,#189147,#189148,#189149,#189150,#189151,
#189152,#189153,#189154,#189155,#189156,#189157,#189158,#189159,#189160,
#189161,#189162,#189163,#189164,#189165,#189166,#189167,#189168,#189169,
#189170,#189171,#189172,#189173,#189174,#189175,#189176,#189177,#189178,
#189179,#189180,#189181,#189182,#189183,#189184,#189185,#189186,#189187,
#189188,#189189,#189190,#189191,#189192,#189193,#189194,#189195,#189196,
#189197,#189198,#189199,#189200,#189201,#189202,#189203,#189204,#189205,
#189206),.UNSPECIFIED.,.F.,.F.,(4,2,2,2,2,2,2,2,2,2,2,2,2,2,2,2,2,2,2,2,
2,2,2,2,2,2,2,2,2,2,2,2,2,2,2,2,2,2,2,2,2,2,2,2,2,2,2,2,2,2,2,2,2,2,2,2,
2,2,2,2,2,2,2,2,2,2,2,2,2,2,2,2,2,2,2,2,2,2,2,2,2,2,2,2,2,2,2,2,2,2,2,2,
2,2,2,2,2,2,2,2,2,2,2,2,2,2,2,2,2,2,4),(1.40857222162858,1.41601196621291,
1.42100658421054,1.437014651322,1.43963419002885,1.44098146932286,1.44205276994169,
1.44330951245523,1.44558352661543,1.45691767558778,1.48293080959558,1.5358538196761,
1.54274968095228,1.54561647356978,1.54740940340059,1.54937076536781,1.55207776171094,
1.55850153445692,1.58712745059703,1.63841311802035,1.64947573332078,1.65162287516071,
1.65297939018676,1.6540513628493,1.65530121610225,1.65754349297141,1.66833947213673,
1.69230077033749,1.74825904843145,1.75488481309453,1.75742427486285,1.75925028425679,
1.76118899524557,1.76376230885916,1.76942731039186,1.79207247719862,1.82489295865303,
1.82941820035558,1.86060916484884,1.86352135013834,1.8649095267517,1.86598429042938,
1.86721244711463,1.8693560986222,1.87866557813956,1.92780721490209,1.96318573935499,
1.96748360549925,1.97002551010166,1.97196619358772,1.97403898214715,1.9772857313156,
1.98758107209317,2.00411095854136,2.036969830897,2.04848618686941,2.05827421766093,
2.0596014028723,2.07316111869237,2.07544388020458,2.07682634267758,2.07790300662812,
2.079120337492,2.08121529030947,2.08987792153073,2.10679402429725,2.1487078611603,
2.17542931454792,2.17954288869872,2.18203092316495,2.18396310590975,2.18605923602294,
2.18941216618977,2.20067145355606,2.21939330033796,2.25481219237785,2.28447589334949,
2.28738994761945,2.28877841742604,2.2898531330865,2.29108092737305,2.29322322625946,
2.30251571352589,2.321353270603,2.36913766416976,2.3880417326222,2.39179138356116,
2.3941963025708,2.39611327166443,2.39827699939892,2.4019352539455,2.41628127405657,
2.46674259933934,2.49644247359409,2.49935661878363,2.50074512832049,2.50181987308139,
2.50304769876655,2.5043394976538,2.50898384579415,2.53311915742372,2.55402308522148,
2.59906813594801,2.60332525106049,2.6058552950734,2.60779401170569,2.60987160570751,
2.61314038063283,2.61694371300853,2.62420850232443,2.66783673935143),
 .UNSPECIFIED.);
#1942=B_SPLINE_CURVE_WITH_KNOTS('',3,(#189207,#189208,#189209,#189210,#189211,
#189212,#189213,#189214,#189215,#189216,#189217,#189218,#189219,#189220,
#189221,#189222,#189223,#189224,#189225,#189226),.UNSPECIFIED.,.F.,.F.,
(4,2,2,2,2,2,2,2,2,4),(0.000649987196025464,0.0375152697788105,0.0412926014893609,
0.0433020283636711,0.0446072096947876,0.0458444130242866,0.0469177254605004,
0.0482917845512197,0.0511320532093311,0.0747588704862031),.UNSPECIFIED.);
#1943=B_SPLINE_CURVE_WITH_KNOTS('',3,(#189232,#189233,#189234,#189235,#189236,
#189237,#189238,#189239,#189240,#189241),.UNSPECIFIED.,.F.,.F.,(4,3,3,4),
(120.689857252469,120.859210445387,120.9625796252,121.040543934877),
 .UNSPECIFIED.);
#1944=B_SPLINE_CURVE_WITH_KNOTS('',3,(#189242,#189243,#189244,#189245,#189246,
#189247,#189248,#189249,#189250,#189251),.UNSPECIFIED.,.F.,.F.,(4,1,1,1,
1,1,1,4),(114.756144625377,114.866191745616,115.865028195577,116.863864645539,
117.862701095501,118.861537545463,119.860373995425,120.689851222923),
 .UNSPECIFIED.);
#1945=B_SPLINE_CURVE_WITH_KNOTS('',3,(#189252,#189253,#189254,#189255,#189256,
#189257,#189258,#189259,#189260,#189261,#189262,#189263,#189264,#189265,
#189266,#189267,#189268,#189269,#189270,#189271,#189272,#189273,#189274,
#189275,#189276,#189277,#189278,#189279,#189280,#189281,#189282,#189283,
#189284,#189285,#189286,#189287,#189288,#189289,#189290,#189291,#189292,
#189293,#189294,#189295,#189296,#189297,#189298,#189299,#189300,#189301,
#189302,#189303,#189304,#189305,#189306,#189307,#189308,#189309,#189310,
#189311,#189312,#189313,#189314,#189315,#189316,#189317,#189318,#189319,
#189320,#189321,#189322,#189323,#189324,#189325,#189326,#189327,#189328,
#189329,#189330,#189331,#189332,#189333,#189334,#189335,#189336,#189337,
#189338,#189339,#189340,#189341,#189342,#189343,#189344,#189345,#189346,
#189347,#189348,#189349,#189350,#189351,#189352,#189353,#189354,#189355,
#189356,#189357,#189358,#189359,#189360,#189361,#189362,#189363,#189364,
#189365,#189366,#189367,#189368,#189369,#189370,#189371,#189372,#189373,
#189374,#189375,#189376,#189377,#189378,#189379,#189380,#189381,#189382,
#189383,#189384,#189385,#189386,#189387,#189388,#189389,#189390,#189391,
#189392,#189393,#189394,#189395,#189396,#189397,#189398,#189399,#189400,
#189401,#189402,#189403,#189404,#189405,#189406,#189407,#189408,#189409,
#189410,#189411,#189412,#189413,#189414,#189415,#189416,#189417,#189418,
#189419,#189420,#189421,#189422,#189423,#189424,#189425,#189426,#189427,
#189428,#189429,#189430,#189431,#189432,#189433,#189434,#189435,#189436,
#189437,#189438,#189439,#189440,#189441,#189442,#189443,#189444,#189445,
#189446,#189447,#189448,#189449,#189450,#189451,#189452,#189453,#189454,
#189455,#189456,#189457,#189458,#189459,#189460,#189461,#189462,#189463,
#189464,#189465,#189466,#189467,#189468,#189469),.UNSPECIFIED.,.F.,.F.,
(4,2,2,2,2,2,2,2,2,2,2,2,2,2,2,2,2,2,2,2,2,2,2,2,2,2,2,2,2,2,2,2,2,2,2,
2,2,2,2,2,2,2,2,2,2,2,2,2,2,2,2,2,2,2,2,2,2,2,2,2,2,2,2,2,2,2,2,2,2,2,2,
2,2,2,2,2,2,2,2,2,2,2,2,2,2,2,2,2,2,2,2,2,2,2,2,2,2,2,2,2,2,2,2,2,2,2,2,
2,4),(0.0747588704862031,0.0879796875914506,0.109399103567414,0.136182009928896,
0.146436010033092,0.149706911363353,0.151785008802629,0.153723604647455,
0.156252646399797,0.160506228968039,0.193184802618462,0.222554041233268,
0.24417378241774,0.254295211425213,0.256485211339123,0.257733365014667,
0.258805366163536,0.260163820267166,0.262835841752181,0.280215848789155,
0.329253311598265,0.347302167883071,0.354571947452605,0.360001949741997,
0.3625673735979,0.364504742840328,0.366332881450401,0.368880760219933,0.375561192794359,
0.430979853898787,0.455321450902922,0.466218687923793,0.468466985392535,
0.469718088090325,0.470789839695392,0.472144411134277,0.474886373864345,
0.493336504876162,0.537461488735937,0.565332010852523,0.571665396941172,
0.574357013475187,0.576315571226138,0.578111713398295,0.580996279706098,
0.588000060041619,0.639382620642811,0.666515110320237,0.678128410191859,
0.680418184617347,0.681678329648746,0.6827493338966,0.684092180189308,0.686691242659467,
0.70221623881318,0.708761595209357,0.722633932417734,0.755493994171886,
0.772056492469513,0.782367914809658,0.785616718771579,0.787690100637495,
0.789630835404042,0.792172080814284,0.796467236253541,0.831578359363654,
0.880465479843008,0.890288671174311,0.892468529653024,0.893704761456567,
0.894778462633567,0.89615462705336,0.899004754680048,0.935374706201895,
0.989163090681777,0.995619143227736,0.998331710887372,1.00029420497743,
1.00208617839788,1.00494710482001,1.01180638461694,1.06524498728573,1.09093524438299,
1.10218664443679,1.10445606215777,1.10571187074455,1.10678335530417,1.10813210827461,
1.11075817318423,1.12692235584457,1.1775803507223,1.20199434029795,1.20789436156687,
1.21051042605123,1.21245612434676,1.21427052072673,1.21676512939122,1.22311497297649,
1.28150396590647,1.30395462180309,1.3143318406434,1.31654824507083,1.31779253084383,
1.31886525492234,1.32022984923615,1.32240325942883,1.33389996252107,1.38263556947134,
1.40832429865576),.UNSPECIFIED.);
#1946=B_SPLINE_CURVE_WITH_KNOTS('',3,(#189475,#189476,#189477,#189478,#189479,
#189480,#189481,#189482),.UNSPECIFIED.,.F.,.F.,(4,2,2,4),(2.59381054906569,
2.59855973280992,2.62659690643914,2.66829332114253),.UNSPECIFIED.);
#1947=B_SPLINE_CURVE_WITH_KNOTS('',3,(#189483,#189484,#189485,#189486,#189487,
#189488,#189489,#189490,#189491,#189492,#189493,#189494,#189495,#189496,
#189497,#189498,#189499,#189500,#189501,#189502,#189503,#189504,#189505,
#189506,#189507,#189508,#189509,#189510,#189511,#189512,#189513,#189514,
#189515,#189516,#189517,#189518,#189519,#189520,#189521,#189522,#189523,
#189524,#189525,#189526,#189527,#189528,#189529,#189530,#189531,#189532,
#189533,#189534,#189535,#189536,#189537,#189538,#189539,#189540,#189541,
#189542,#189543,#189544,#189545,#189546,#189547,#189548,#189549,#189550,
#189551,#189552,#189553,#189554,#189555,#189556,#189557,#189558,#189559,
#189560,#189561,#189562,#189563,#189564,#189565,#189566,#189567,#189568,
#189569,#189570,#189571,#189572,#189573,#189574,#189575,#189576,#189577,
#189578,#189579,#189580,#189581,#189582,#189583,#189584,#189585,#189586,
#189587,#189588,#189589,#189590,#189591,#189592,#189593,#189594,#189595,
#189596,#189597,#189598,#189599,#189600,#189601,#189602,#189603,#189604,
#189605,#189606,#189607,#189608,#189609,#189610,#189611,#189612,#189613,
#189614,#189615,#189616,#189617,#189618,#189619,#189620,#189621,#189622,
#189623,#189624,#189625,#189626,#189627,#189628,#189629,#189630,#189631,
#189632,#189633,#189634,#189635,#189636,#189637,#189638,#189639,#189640,
#189641,#189642,#189643,#189644,#189645,#189646,#189647,#189648,#189649,
#189650,#189651,#189652,#189653,#189654,#189655,#189656,#189657,#189658,
#189659,#189660),.UNSPECIFIED.,.F.,.F.,(4,3,3,3,3,3,3,3,3,3,3,3,3,3,3,3,
3,3,3,3,3,3,3,3,3,3,3,3,3,3,3,3,3,3,3,3,3,3,3,3,3,3,3,3,3,3,3,3,3,3,3,3,
3,3,3,3,3,3,3,4),(121.040543934877,121.143685143129,121.246752596576,121.34978034831,
121.452802399964,121.555926023838,121.659098486548,121.76246199832,121.858046895349,
121.961441632397,122.064682914512,122.167802879905,122.270857448114,122.373880656472,
122.476906499145,122.580039265923,122.683228357333,122.786600350715,122.856883345311,
122.960278082359,123.063519364473,123.166639329865,123.269693898074,123.372717106431,
123.475742949104,123.578875715881,123.682064807291,123.785436800672,123.855719795272,
123.95911453232,124.062355814435,124.165475779827,124.268530348036,124.371553556394,
124.474579399066,124.577712165844,124.680901257254,124.784273250635,124.854556245234,
124.957950982282,125.061192264397,125.16431222979,125.267366797999,125.370390006357,
125.473415849029,125.576548615808,125.679737707218,125.7831097006,125.853392695196,
125.956787432244,126.060028714359,126.163148679752,126.266203247961,126.369226456318,
126.472252298991,126.575385065769,126.678574157179,126.781946150561,126.852229145158,
126.973042559648),.UNSPECIFIED.);
#1948=B_SPLINE_CURVE_WITH_KNOTS('',3,(#189662,#189663,#189664,#189665,#189666,
#189667,#189668,#189669,#189670,#189671,#189672,#189673,#189674,#189675,
#189676,#189677,#189678,#189679,#189680,#189681,#189682,#189683,#189684,
#189685,#189686,#189687,#189688,#189689,#189690,#189691,#189692,#189693,
#189694,#189695,#189696,#189697,#189698,#189699,#189700,#189701,#189702,
#189703,#189704,#189705,#189706,#189707,#189708,#189709,#189710,#189711,
#189712,#189713,#189714,#189715,#189716,#189717,#189718,#189719,#189720,
#189721,#189722,#189723,#189724,#189725,#189726,#189727,#189728,#189729,
#189730,#189731,#189732,#189733,#189734,#189735,#189736,#189737,#189738,
#189739,#189740,#189741,#189742,#189743,#189744,#189745,#189746,#189747,
#189748,#189749,#189750,#189751,#189752,#189753,#189754,#189755,#189756,
#189757,#189758,#189759,#189760,#189761,#189762,#189763,#189764,#189765,
#189766,#189767,#189768,#189769,#189770,#189771,#189772,#189773,#189774,
#189775,#189776,#189777,#189778,#189779,#189780,#189781,#189782,#189783,
#189784,#189785,#189786,#189787,#189788,#189789,#189790,#189791,#189792,
#189793,#189794,#189795,#189796,#189797,#189798,#189799,#189800,#189801,
#189802,#189803,#189804,#189805,#189806,#189807,#189808,#189809,#189810,
#189811,#189812,#189813,#189814,#189815,#189816,#189817,#189818,#189819,
#189820,#189821,#189822,#189823,#189824,#189825,#189826,#189827,#189828,
#189829,#189830,#189831,#189832,#189833,#189834,#189835,#189836,#189837,
#189838,#189839,#189840,#189841,#189842,#189843,#189844,#189845,#189846,
#189847,#189848,#189849,#189850,#189851,#189852,#189853,#189854,#189855,
#189856,#189857,#189858,#189859,#189860,#189861,#189862,#189863,#189864,
#189865,#189866,#189867,#189868,#189869,#189870,#189871,#189872,#189873,
#189874,#189875,#189876,#189877,#189878,#189879),.UNSPECIFIED.,.F.,.F.,
(4,2,2,2,2,2,2,2,2,2,2,2,2,2,2,2,2,2,2,2,2,2,2,2,2,2,2,2,2,2,2,2,2,2,2,
2,2,2,2,2,2,2,2,2,2,2,2,2,2,2,2,2,2,2,2,2,2,2,2,2,2,2,2,2,2,2,2,2,2,2,2,
2,2,2,2,2,2,2,2,2,2,2,2,2,2,2,2,2,2,2,2,2,2,2,2,2,2,2,2,2,2,2,2,2,2,2,2,
2,4),(1.40832429865576,1.41583884495366,1.42010269900384,1.42263499019131,
1.42457441055375,1.42665176571331,1.42991807626368,1.44038113715901,1.45728208869256,
1.49511037488455,1.52518599045843,1.52810058168737,1.52948935833352,1.53056433495725,
1.53179245361094,1.53393537987583,1.5432315357883,1.56207807729296,1.60247855317451,
1.61474064742621,1.62934649342146,1.63313477184721,1.63534976156614,1.63726202080289,
1.63959705037182,1.64404697230231,1.67495966336917,1.72180621505924,1.73760405313658,
1.74021653802424,1.74156242286277,1.74263379219851,1.74389198196789,1.74617209712654,
1.75760866537589,1.78402402621373,1.83638785391721,1.84332628260559,1.84620035967748,
1.8479948190856,1.84995542820426,1.85265694773325,1.85904680520332,1.88738511825063,
1.93728516006437,1.94991466861279,1.95215090234824,1.95353452095267,1.95460902866221,
1.95584056691653,1.95799878037093,1.96750764192813,2.01664208994934,2.05182819066386,
2.0561245499724,2.05866631176982,2.06060731715934,2.0626808672741,2.06592968129853,
2.0762389137514,2.09279808800999,2.12568565054142,2.13955221159419,2.14611376194883,
2.16166407760683,2.16426452046228,2.1656077630128,2.16667891497163,2.16793904323441,
2.17022828823725,2.18182888435915,2.20890480585537,2.2603364903594,2.26733515714113,
2.27021909701194,2.27201528838317,2.27397425599951,2.27666707605165,2.2830062603409,
2.31092520737643,2.35694097730278,2.35794187149938,2.37366921516647,2.37627720144427,
2.37762207054712,2.37869331907723,2.37995216593099,2.38223551275641,2.39373092527518,
2.42038248370029,2.47238243700029,2.47936146681885,2.48224214585815,2.48403773500581,
2.48585833958336,2.48841277472039,2.49401322600401,2.50153647292751,2.52050598213682,
2.54851777748622,2.58534456122477,2.58818630672239,2.58956080069349,2.59063431748126,
2.59187161139157,2.5940563912719,2.60395325166763,2.65275138022529,2.66750909677174),
 .UNSPECIFIED.);
#1949=B_SPLINE_CURVE_WITH_KNOTS('',3,(#189880,#189881,#189882,#189883,#189884,
#189885,#189886,#189887,#189888,#189889,#189890,#189891,#189892,#189893,
#189894,#189895,#189896,#189897,#189898,#189899,#189900,#189901),
 .UNSPECIFIED.,.F.,.F.,(4,2,2,2,2,2,2,2,2,2,4),(0.000768647970570284,0.0217309695992682,
0.0248341065116262,0.0269704254049385,0.0287696705523692,0.0306848619291281,
0.0330687978124981,0.0367500452676532,0.0545887181713197,0.072975494517195,
0.0751664090908324),.UNSPECIFIED.);
#1950=B_SPLINE_CURVE_WITH_KNOTS('',3,(#189906,#189907,#189908,#189909,#189910,
#189911,#189912,#189913,#189914,#189915,#189916,#189917,#189918,#189919,
#189920,#189921,#189922,#189923,#189924,#189925,#189926,#189927,#189928,
#189929,#189930,#189931,#189932,#189933,#189934,#189935,#189936,#189937,
#189938,#189939,#189940,#189941,#189942,#189943,#189944,#189945,#189946,
#189947,#189948,#189949,#189950,#189951,#189952,#189953,#189954,#189955,
#189956,#189957,#189958,#189959,#189960,#189961,#189962,#189963,#189964,
#189965,#189966,#189967,#189968,#189969,#189970,#189971,#189972,#189973,
#189974,#189975,#189976,#189977,#189978,#189979,#189980,#189981,#189982,
#189983,#189984,#189985,#189986,#189987,#189988,#189989,#189990,#189991,
#189992,#189993,#189994,#189995,#189996,#189997,#189998,#189999,#190000,
#190001,#190002,#190003,#190004,#190005,#190006,#190007,#190008,#190009,
#190010,#190011,#190012,#190013,#190014,#190015,#190016,#190017,#190018,
#190019,#190020,#190021,#190022,#190023,#190024,#190025,#190026,#190027,
#190028,#190029,#190030,#190031,#190032,#190033,#190034,#190035,#190036,
#190037,#190038,#190039,#190040,#190041,#190042,#190043,#190044,#190045,
#190046,#190047,#190048,#190049,#190050,#190051,#190052,#190053,#190054,
#190055,#190056,#190057,#190058,#190059,#190060,#190061,#190062,#190063,
#190064,#190065,#190066,#190067,#190068,#190069,#190070,#190071,#190072,
#190073,#190074,#190075,#190076,#190077,#190078,#190079,#190080,#190081,
#190082,#190083,#190084,#190085,#190086,#190087,#190088,#190089,#190090,
#190091,#190092,#190093,#190094,#190095,#190096,#190097,#190098,#190099,
#190100,#190101,#190102,#190103,#190104,#190105,#190106,#190107,#190108,
#190109,#190110,#190111,#190112,#190113,#190114,#190115,#190116,#190117,
#190118,#190119,#190120,#190121,#190122,#190123,#190124,#190125,#190126,
#190127,#190128,#190129,#190130,#190131,#190132,#190133,#190134,#190135,
#190136,#190137,#190138,#190139,#190140,#190141,#190142,#190143),
 .UNSPECIFIED.,.F.,.F.,(4,2,2,2,2,2,2,2,2,2,2,2,2,2,2,2,2,2,2,2,2,2,2,2,
2,2,2,2,2,2,2,2,2,2,2,2,2,2,2,2,2,2,2,2,2,2,2,2,2,2,2,2,2,2,2,2,2,2,2,2,
2,2,2,2,2,2,2,2,2,2,2,2,2,2,2,2,2,2,2,2,2,2,2,2,2,2,2,2,2,2,2,2,2,2,2,2,
2,2,2,2,2,2,2,2,2,2,2,2,2,2,2,2,2,2,2,2,2,2,4),(1.25997183052399,1.27817567886033,
1.30767952852,1.31208995429294,1.31441688987609,1.31614398429107,1.31830042104015,
1.32192326049702,1.33437403324548,1.38533491188035,1.41654472381099,1.41945791182565,
1.42084657011798,1.42192170843108,1.42315029513985,1.42529470172456,1.43460753016451,
1.48376662632684,1.51915704870962,1.52345640857122,1.52599919825571,1.52794055843185,
1.530014070669,1.53326195531548,1.54356091300877,1.56009662248404,1.59296700102857,
1.60449381399583,1.6142450350421,1.61616610662091,1.62921742622787,1.63147548843054,
1.63286570439141,1.63394093797432,1.63516839264351,1.6373079222005,1.64655496320553,
1.66524609360828,1.70943437688544,1.73180205662411,1.73574128667566,1.73820443755014,
1.74012828189235,1.74225893361626,1.74576560970272,1.75856932078564,1.78108185957412,
1.82960357948144,1.84136212302166,1.84355430743698,1.84492468045176,1.84599801655695,
1.84723855163952,1.84943739922561,1.8595409327925,1.88103622391695,1.89337486426171,
1.93941064742755,1.94661835591445,1.94953755001237,1.95134045154839,1.95329471689711,
1.95595943690022,1.96213363241734,1.98870292006014,2.02808114368097,2.03941483875518,
2.05318730589606,2.05548100874553,2.05686696227646,2.05794439586525,2.05916040305897,
2.06124811942227,2.06981204916858,2.08643464813904,2.12835895507403,2.15549366223038,
2.15961898976107,2.16211095757247,2.16404430804365,2.1661398176675,2.16948765594565,
2.18069127297986,2.19928025092611,2.24261624307531,2.26472797766188,2.26756700696273,
2.26894112952305,2.2700148019016,2.27125277976661,2.2734399821749,2.28336833585192,
2.33215167780638,2.3672266941228,2.37152191997075,2.37406346338802,2.37600456246437,
2.37807846521967,2.38132835914815,2.39164546519976,2.4082215187391,2.47085804352185,
2.47221932342294,2.47838898108063,2.48032696053338,2.48150973046551,2.48254141104951,
2.48395478344332,2.48697107807225,2.49107129277855,2.50135666515076,2.52417539952219,
2.57588652624925,2.58287117880116,2.58575330931771,2.58754954685035,2.58950950137706,
2.59220538333982,2.59381054906569),.UNSPECIFIED.);
#1951=B_SPLINE_CURVE_WITH_KNOTS('',3,(#190144,#190145,#190146,#190147,#190148,
#190149,#190150,#190151,#190152,#190153,#190154,#190155,#190156,#190157,
#190158,#190159,#190160,#190161,#190162,#190163,#190164,#190165,#190166,
#190167,#190168,#190169,#190170,#190171,#190172,#190173,#190174,#190175,
#190176,#190177,#190178,#190179,#190180,#190181,#190182,#190183,#190184,
#190185,#190186,#190187,#190188,#190189,#190190,#190191,#190192,#190193,
#190194,#190195,#190196,#190197,#190198,#190199,#190200,#190201,#190202,
#190203,#190204,#190205,#190206,#190207,#190208,#190209,#190210,#190211,
#190212,#190213,#190214,#190215,#190216,#190217,#190218,#190219,#190220,
#190221,#190222,#190223,#190224,#190225,#190226,#190227,#190228,#190229,
#190230,#190231,#190232,#190233,#190234,#190235,#190236,#190237,#190238,
#190239,#190240,#190241,#190242,#190243,#190244,#190245,#190246,#190247,
#190248,#190249,#190250,#190251,#190252,#190253,#190254,#190255,#190256,
#190257,#190258,#190259,#190260,#190261,#190262,#190263,#190264,#190265,
#190266,#190267,#190268,#190269,#190270,#190271,#190272,#190273,#190274,
#190275,#190276,#190277,#190278,#190279,#190280,#190281,#190282,#190283,
#190284,#190285,#190286,#190287,#190288,#190289,#190290,#190291,#190292,
#190293,#190294,#190295,#190296,#190297,#190298,#190299,#190300,#190301,
#190302,#190303,#190304,#190305,#190306,#190307,#190308,#190309,#190310,
#190311,#190312,#190313,#190314,#190315,#190316,#190317,#190318,#190319,
#190320,#190321,#190322,#190323,#190324,#190325,#190326,#190327,#190328,
#190329,#190330,#190331,#190332,#190333,#190334,#190335,#190336,#190337,
#190338,#190339,#190340,#190341,#190342,#190343,#190344,#190345,#190346,
#190347,#190348,#190349,#190350,#190351,#190352,#190353,#190354,#190355,
#190356,#190357,#190358,#190359,#190360,#190361,#190362,#190363,#190364,
#190365,#190366,#190367,#190368,#190369,#190370,#190371,#190372,#190373,
#190374,#190375,#190376,#190377),.UNSPECIFIED.,.F.,.F.,(4,2,2,2,2,2,2,2,
2,2,2,2,2,2,2,2,2,2,2,2,2,2,2,2,2,2,2,2,2,2,2,2,2,2,2,2,2,2,2,2,2,2,2,2,
2,2,2,2,2,2,2,2,2,2,2,2,2,2,2,2,2,2,2,2,2,2,2,2,2,2,2,2,2,2,2,2,2,2,2,2,
2,2,2,2,2,2,2,2,2,2,2,2,2,2,2,2,2,2,2,2,2,2,2,2,2,2,2,2,2,2,2,2,2,2,2,2,
4),(0.0751664090908324,0.121837060794992,0.131681154580003,0.133862218936931,
0.135098609348292,0.136172112973235,0.137547586555477,0.14039478308759,
0.176867593743613,0.209428589603404,0.225633494276976,0.232378372999333,
0.237517835267561,0.239980362266982,0.24182160906685,0.243648984947873,
0.24619358731576,0.252852041300881,0.308507478827018,0.332697662164898,
0.343554696200585,0.345800715641859,0.347051391175338,0.348123294323277,
0.349478720652284,0.351622253527715,0.362626804254524,0.413891793790983,
0.442557477613195,0.448986593123129,0.451694562979244,0.453656168813981,
0.455449007921287,0.45831496133963,0.465205183335653,0.51824131493154,0.544208668875459,
0.555530763501977,0.557804197079648,0.559060850781458,0.560132220078928,
0.561479763280902,0.564100338996175,0.580124041799767,0.585198357313938,
0.62988200363044,0.648403689166925,0.659578942020468,0.662923333421311,
0.665017817799912,0.666950992464238,0.669443811657874,0.673572910091847,
0.700868879448593,0.743120553968538,0.759406863082676,0.767853959244599,
0.769932121744742,0.771145872170893,0.772223552155801,0.773612714392369,
0.775917733466,0.789930520496486,0.791300161058096,0.798313730845986,0.81198834179328,
0.844849354606316,0.861410892866797,0.871722138504353,0.874971110813799,
0.877044653944802,0.878985577468383,0.881527124593694,0.885822912254324,
0.920955318573848,0.969901902909867,0.979660706696958,0.981836311782615,
0.983071678036541,0.984145617251088,0.985523380514225,0.988381267646278,
1.01124168745723,1.0240066975221,1.05686244976068,1.07341519163896,1.08372275748767,
1.08697152690445,1.08904517046851,1.09098634953222,1.09352846436847,1.09782573412167,
1.13304047776493,1.18224589602785,1.19170985580366,1.19386507805123,1.1950960392592,
1.19617078041621,1.19755565845216,1.19979579758883,1.21249724423315,1.23487538868016,
1.26847905280066,1.29385628229564,1.29812698963818,1.30042452392246,1.30231759679482,
1.30455834273101,1.30845750771934,1.32436621245914,1.3345884709149,1.37387287164785,
1.40245709083406,1.40536964828917,1.40675819973767,1.40783334453758,1.40876522934455),
 .UNSPECIFIED.);
#1952=B_SPLINE_CURVE_WITH_KNOTS('',3,(#190383,#190384,#190385,#190386,#190387,
#190388,#190389,#190390,#190391,#190392,#190393,#190394,#190395,#190396,
#190397,#190398,#190399,#190400,#190401,#190402,#190403,#190404),
 .UNSPECIFIED.,.F.,.F.,(4,2,2,2,2,2,2,2,2,2,4),(2.59301342310063,2.59652018861172,
2.60119783305151,2.60293253192801,2.60395677895129,2.60504993697695,2.60656487605862,
2.61017450132261,2.61524686047379,2.62925650837804,2.66711449156562),
 .UNSPECIFIED.);
#1953=B_SPLINE_CURVE_WITH_KNOTS('',3,(#190405,#190406,#190407,#190408,#190409,
#190410,#190411,#190412,#190413,#190414,#190415,#190416,#190417,#190418,
#190419,#190420,#190421,#190422,#190423,#190424,#190425,#190426,#190427,
#190428,#190429,#190430,#190431,#190432,#190433,#190434,#190435,#190436,
#190437,#190438,#190439,#190440,#190441,#190442,#190443,#190444,#190445,
#190446,#190447,#190448,#190449,#190450,#190451,#190452,#190453,#190454,
#190455,#190456,#190457,#190458,#190459,#190460,#190461,#190462,#190463,
#190464,#190465,#190466,#190467,#190468,#190469,#190470,#190471,#190472,
#190473,#190474,#190475,#190476,#190477,#190478,#190479,#190480,#190481,
#190482,#190483,#190484,#190485,#190486,#190487,#190488,#190489,#190490,
#190491,#190492,#190493,#190494,#190495,#190496,#190497,#190498,#190499,
#190500,#190501,#190502,#190503,#190504,#190505,#190506,#190507,#190508,
#190509,#190510,#190511,#190512,#190513,#190514,#190515,#190516,#190517,
#190518,#190519,#190520,#190521,#190522,#190523,#190524,#190525,#190526,
#190527,#190528,#190529,#190530,#190531,#190532,#190533,#190534,#190535,
#190536,#190537,#190538,#190539,#190540,#190541,#190542,#190543,#190544,
#190545,#190546,#190547,#190548,#190549,#190550,#190551,#190552,#190553,
#190554,#190555,#190556,#190557,#190558,#190559,#190560,#190561,#190562,
#190563,#190564,#190565,#190566,#190567,#190568,#190569,#190570,#190571,
#190572,#190573,#190574,#190575,#190576,#190577,#190578,#190579,#190580,
#190581,#190582,#190583,#190584,#190585,#190586,#190587,#190588,#190589,
#190590,#190591,#190592,#190593,#190594,#190595,#190596,#190597,#190598,
#190599,#190600,#190601,#190602,#190603,#190604,#190605,#190606,#190607,
#190608,#190609,#190610,#190611,#190612,#190613,#190614,#190615,#190616,
#190617,#190618,#190619,#190620,#190621,#190622,#190623,#190624,#190625,
#190626,#190627,#190628,#190629,#190630,#190631,#190632),.UNSPECIFIED.,
 .F.,.F.,(4,2,2,2,2,2,2,2,2,2,2,2,2,2,2,2,2,2,2,2,2,2,2,2,2,2,2,2,2,2,2,
2,2,2,2,2,2,2,2,2,2,2,2,2,2,2,2,2,2,2,2,2,2,2,2,2,2,2,2,2,2,2,2,2,2,2,2,
2,2,2,2,2,2,2,2,2,2,2,2,2,2,2,2,2,2,2,2,2,2,2,2,2,2,2,2,2,2,2,2,2,2,2,2,
2,2,2,2,2,2,2,2,2,2,4),(0.00070417365456507,0.0257174857516651,0.0359847480784371,
0.0390635037060503,0.0411898132628437,0.0432709727765218,0.0452083303494675,
0.047729912948974,0.0519580123236602,0.0833470854812081,0.108660532403853,
0.136506496715738,0.145896845031396,0.148046207237502,0.149275561060278,
0.150350028422841,0.151736041141806,0.153980938539433,0.166786704522338,
0.188793015005292,0.215577358353407,0.23704354853604,0.245226816600629,
0.251216700447995,0.253840413141923,0.255796348256697,0.257595616110479,
0.260497421472034,0.267604938409068,0.317187172083802,0.355583624564653,
0.35916926711615,0.360680067198888,0.361772446643604,0.362797722533406,
0.364537908087725,0.369252155315286,0.409787642162989,0.456725506184692,
0.463118884531493,0.465820692809186,0.467781076220977,0.469575032644453,
0.472447645198868,0.479379118298607,0.531842815258053,0.558206612602061,
0.569628710827241,0.571907734651659,0.573165546103371,0.574236732239752,
0.575582557494768,0.578195428008421,0.59405582464407,0.598862688444337,
0.614071685277517,0.646946957225565,0.663527873732877,0.673847616726631,
0.67709736954593,0.679170955349841,0.681111598982654,0.683652318260893,
0.687945672940657,0.730339605970443,0.759384712515066,0.774118772814738,
0.782015001040382,0.784047244550115,0.785250749405223,0.786330812000847,
0.787738083619861,0.790105073647513,0.805531936840359,0.812269412497604,
0.826058617288149,0.858919141486843,0.875481262202823,0.885792628402886,
0.88904150998083,0.891114964285735,0.893055782947641,0.895597161431638,
0.8998925938382,0.935012840958341,0.983925279081658,0.993721128804179,0.995899188165928,
0.997135055486108,0.998208859356632,0.999585703072175,1.00243911823943,
1.02512457408904,1.03806473222202,1.07092042002931,1.08747426149498,1.09778218132457,
1.10103088630441,1.1031044464417,1.10504551769378,1.10758744846606,1.1118843109584,
1.14708264797785,1.19623652119962,1.20575655406218,1.20791566285735,1.20914744164461,
1.21022198959788,1.21160542700361,1.21384090211796,1.22645486852707,1.23298050298514,
1.23811264297844,1.25997183052399),.UNSPECIFIED.);
#1954=B_SPLINE_CURVE_WITH_KNOTS('',3,(#190634,#190635,#190636,#190637,#190638,
#190639,#190640,#190641,#190642,#190643,#190644,#190645,#190646,#190647,
#190648,#190649,#190650,#190651,#190652,#190653,#190654,#190655,#190656,
#190657,#190658,#190659,#190660,#190661,#190662,#190663,#190664,#190665,
#190666,#190667,#190668,#190669,#190670,#190671,#190672,#190673,#190674,
#190675,#190676,#190677,#190678,#190679,#190680,#190681,#190682,#190683,
#190684,#190685,#190686,#190687,#190688,#190689,#190690,#190691,#190692,
#190693,#190694,#190695,#190696,#190697,#190698,#190699,#190700,#190701,
#190702,#190703,#190704,#190705,#190706,#190707,#190708,#190709,#190710,
#190711,#190712,#190713,#190714,#190715,#190716,#190717,#190718,#190719,
#190720,#190721,#190722,#190723,#190724,#190725,#190726,#190727,#190728,
#190729,#190730,#190731,#190732,#190733,#190734,#190735,#190736,#190737,
#190738,#190739,#190740,#190741,#190742,#190743,#190744,#190745,#190746,
#190747,#190748,#190749,#190750,#190751,#190752,#190753,#190754,#190755,
#190756,#190757,#190758,#190759,#190760,#190761,#190762,#190763,#190764,
#190765,#190766,#190767,#190768,#190769,#190770,#190771,#190772,#190773,
#190774,#190775,#190776,#190777,#190778,#190779,#190780,#190781,#190782,
#190783,#190784,#190785,#190786,#190787,#190788,#190789,#190790,#190791,
#190792,#190793,#190794,#190795,#190796,#190797,#190798,#190799,#190800,
#190801,#190802,#190803,#190804,#190805,#190806,#190807,#190808,#190809,
#190810,#190811,#190812,#190813,#190814,#190815,#190816,#190817,#190818,
#190819,#190820,#190821,#190822,#190823,#190824,#190825,#190826,#190827,
#190828,#190829,#190830,#190831,#190832,#190833,#190834,#190835,#190836,
#190837,#190838,#190839,#190840,#190841,#190842,#190843,#190844,#190845,
#190846,#190847,#190848,#190849,#190850,#190851,#190852,#190853,#190854,
#190855,#190856,#190857,#190858,#190859,#190860,#190861,#190862,#190863),
 .UNSPECIFIED.,.F.,.F.,(4,2,2,2,2,2,2,2,2,2,2,2,2,2,2,2,2,2,2,2,2,2,2,2,
2,2,2,2,2,2,2,2,2,2,2,2,2,2,2,2,2,2,2,2,2,2,2,2,2,2,2,2,2,2,2,2,2,2,2,2,
2,2,2,2,2,2,2,2,2,2,2,2,2,2,2,2,2,2,2,2,2,2,2,2,2,2,2,2,2,2,2,2,2,2,2,2,
2,2,2,2,2,2,2,2,2,2,2,2,2,2,2,2,2,2,4),(1.40876522934455,1.40906203844239,
1.41120686592205,1.42052513857405,1.46970161231669,1.50507080576657,1.50936998566118,
1.51191274775594,1.51385413225212,1.51592771444487,1.51917580043562,1.52947616880855,
1.54601487666193,1.57356167837748,1.58970409347244,1.600784706932,1.61502053685379,
1.61733716480446,1.6187298518975,1.61980813026777,1.62102017469625,1.62309008558368,
1.63143247862436,1.64741379441942,1.68972807553654,1.71734565740105,1.72148337964582,
1.72397896862389,1.72591283649619,1.72800661944552,1.73134674439907,1.74247829120265,
1.76089970967477,1.80770742523714,1.81252956966111,1.82701168344094,1.82934218372271,
1.83073895560801,1.83181778964995,1.83302754926357,1.83508710443475,1.84330297118474,
1.85892394604438,1.90067235665691,1.92931450646513,1.93347935906925,1.93598293615531,
1.93791805149379,1.94000827353765,1.94333213529409,1.95431205570459,1.97238290730774,
2.02252301941893,2.0389114593475,2.04154695669813,2.04289790616715,2.04396974959826,
2.04522438244351,2.04748762883996,2.05862750092203,2.08387991806958,2.13793358711759,
2.14474145305826,2.14759426382349,2.14938504870012,2.15134939482114,2.15407032808689,
2.16057405870037,2.18986706413482,2.23045248167066,2.25076712538338,2.25356035354298,
2.25492541685537,2.25599829628312,2.25724252614575,2.25945823948905,2.26982198919262,
2.2922207410463,2.35066402619404,2.35700471302507,2.35949796515481,2.36131215931685,
2.36325837857622,2.36587642437814,2.37178639337514,2.39627727351485,2.44388131991961,
2.46288674951732,2.46565098712122,2.46701024350062,2.46805186727489,2.46805591400501,
2.46805989278188,2.4680638049572,2.46806765199019,2.46807124430431,2.46807482310213,
2.46807838865476,2.46808194093323,2.46930494281057,2.47061534797828,2.47263693893703,
2.47644584213214,2.48570633250583,2.52347010312493,2.5337534772937,2.56534492805526,
2.56957833020121,2.57210195237765,2.57404021221258,2.57612168825699,2.57940580955971,
2.59002433475977,2.60727269931124,2.6683774093147),.UNSPECIFIED.);
#1955=B_SPLINE_CURVE_WITH_KNOTS('',3,(#190864,#190865,#190866,#190867,#190868,
#190869,#190870,#190871,#190872,#190873,#190874,#190875,#190876,#190877,
#190878,#190879,#190880,#190881,#190882,#190883,#190884,#190885,#190886,
#190887),.UNSPECIFIED.,.F.,.F.,(4,2,2,2,2,2,2,2,2,2,2,4),(0.000810717560574591,
0.00554260829355552,0.00881068920855145,0.010244569293212,0.0113189780628067,
0.0123417944517917,0.0133649961849808,0.0148060120350927,0.0186526100510774,
0.0263910001425551,0.0473308873917541,0.0750288866695304),.UNSPECIFIED.);
#1956=B_SPLINE_CURVE_WITH_KNOTS('',3,(#190892,#190893,#190894,#190895,#190896,
#190897,#190898,#190899,#190900,#190901,#190902,#190903,#190904,#190905,
#190906,#190907,#190908,#190909,#190910,#190911,#190912,#190913,#190914,
#190915,#190916,#190917,#190918,#190919,#190920,#190921,#190922,#190923,
#190924,#190925,#190926,#190927,#190928,#190929,#190930,#190931,#190932,
#190933,#190934,#190935,#190936,#190937,#190938,#190939,#190940,#190941,
#190942,#190943,#190944,#190945,#190946,#190947,#190948,#190949,#190950,
#190951,#190952,#190953,#190954,#190955,#190956,#190957,#190958,#190959,
#190960,#190961,#190962,#190963,#190964,#190965,#190966,#190967,#190968,
#190969,#190970,#190971,#190972,#190973,#190974,#190975,#190976,#190977,
#190978,#190979,#190980,#190981,#190982,#190983,#190984,#190985,#190986,
#190987,#190988,#190989,#190990,#190991,#190992,#190993,#190994,#190995,
#190996,#190997,#190998,#190999,#191000,#191001,#191002,#191003,#191004,
#191005,#191006,#191007,#191008,#191009,#191010,#191011,#191012,#191013,
#191014,#191015,#191016,#191017,#191018,#191019,#191020,#191021,#191022,
#191023,#191024,#191025,#191026,#191027,#191028,#191029,#191030,#191031,
#191032,#191033,#191034,#191035,#191036,#191037,#191038,#191039,#191040,
#191041,#191042,#191043,#191044,#191045,#191046,#191047,#191048,#191049,
#191050,#191051,#191052,#191053,#191054,#191055,#191056,#191057,#191058,
#191059,#191060,#191061,#191062,#191063,#191064,#191065,#191066,#191067,
#191068,#191069,#191070,#191071,#191072,#191073,#191074,#191075,#191076,
#191077,#191078,#191079,#191080,#191081,#191082,#191083,#191084,#191085,
#191086,#191087,#191088,#191089,#191090,#191091,#191092,#191093,#191094,
#191095,#191096,#191097,#191098,#191099,#191100,#191101,#191102,#191103,
#191104,#191105,#191106,#191107,#191108,#191109,#191110,#191111,#191112,
#191113,#191114,#191115,#191116,#191117,#191118,#191119,#191120,#191121,
#191122,#191123,#191124,#191125,#191126,#191127),.UNSPECIFIED.,.F.,.F.,
(4,2,2,2,2,2,2,2,2,2,2,2,2,2,2,2,2,2,2,2,2,2,2,2,2,2,2,2,2,2,2,2,2,2,2,
2,2,2,2,2,2,2,2,2,2,2,2,2,2,2,2,2,2,2,2,2,2,2,2,2,2,2,2,2,2,2,2,2,2,2,2,
2,2,2,2,2,2,2,2,2,2,2,2,2,2,2,2,2,2,2,2,2,2,2,2,2,2,2,2,2,2,2,2,2,2,2,2,
2,2,2,2,2,2,2,2,2,2,4),(1.25961098705092,1.26429589096183,1.30523587040568,
1.32771330738116,1.3303764594605,1.33171516128731,1.33268303899733,1.33390652731652,
1.33602883137143,1.34504661564238,1.36302990581967,1.4132405423344,1.43104246885246,
1.43472154572487,1.43710492851623,1.43902022329457,1.44119876054537,1.44492321875558,
1.46032818122401,1.51165837432783,1.53933387157848,1.54224052694126,1.54362769569379,
1.5447024298606,1.54593139333262,1.54807842483266,1.55743318582157,1.60669366318553,
1.64191346431821,1.64620969238522,1.6487512269324,1.65069197264094,1.65276516183558,
1.65601323605462,1.66631865223905,1.68287030021161,1.7157488117304,1.72919468933446,
1.73677775908984,1.75177426042052,1.75412354904193,1.75552560648424,1.75660488848266,
1.7578111116667,1.7598557678916,1.76789843774536,1.78303562077719,1.82273162969494,
1.85396941562139,1.85819439583057,1.86071517094643,1.86265251122501,1.86473424315566,
1.86802140340636,1.878672876719,1.89599752699931,1.94418960827059,1.94848458820401,
1.95083866934147,1.96390018632466,1.96615838982003,1.96754848096143,1.96862348349695,
1.9698505241838,1.9719889813816,1.98122602067255,1.99988824328324,2.04403206465749,
2.06645691093807,2.07039789313005,2.07286127560859,2.07478476557204,2.07691447785506,
2.08041834899328,2.09319772888885,2.11565000635428,2.15606158561172,2.16038645969957,
2.16186163765369,2.17577409847162,2.17807413266991,2.17946175981933,2.18053916068743,
2.18175363234102,2.18383533974423,2.1923284498817,2.20874672700626,2.25239703387108,
2.26464294689534,2.2793373993013,2.28313315344194,2.28534967396721,2.28726154038849,
2.28959393805035,2.29403223713569,2.32453851236181,2.36816434175097,2.37249180629,
2.37697490893965,2.38801865868004,2.39016459163177,2.39152071783719,2.39259263339461,
2.39384270772542,2.39608609885265,2.40690117302882,2.43093356853466,2.47256911358986,
2.49080658172696,2.49451338717382,2.49690533514595,2.49882139043036,2.500620088583,
2.50374313045043,2.51354125425459,2.5290804575828,2.55074369450569,2.59301342310063),
 .UNSPECIFIED.);
#1957=B_SPLINE_CURVE_WITH_KNOTS('',3,(#191128,#191129,#191130,#191131,#191132,
#191133,#191134,#191135,#191136,#191137,#191138,#191139,#191140,#191141,
#191142,#191143,#191144,#191145,#191146,#191147,#191148,#191149,#191150,
#191151,#191152,#191153,#191154,#191155,#191156,#191157,#191158,#191159,
#191160,#191161,#191162,#191163,#191164,#191165,#191166,#191167,#191168,
#191169,#191170,#191171,#191172,#191173,#191174,#191175,#191176,#191177,
#191178,#191179,#191180,#191181,#191182,#191183,#191184,#191185,#191186,
#191187,#191188,#191189,#191190,#191191,#191192,#191193,#191194,#191195,
#191196,#191197,#191198,#191199,#191200,#191201,#191202,#191203,#191204,
#191205,#191206,#191207,#191208,#191209,#191210,#191211,#191212,#191213,
#191214,#191215,#191216,#191217,#191218,#191219,#191220,#191221,#191222,
#191223,#191224,#191225,#191226,#191227,#191228,#191229,#191230,#191231,
#191232,#191233,#191234,#191235,#191236,#191237,#191238,#191239,#191240,
#191241,#191242,#191243,#191244,#191245,#191246,#191247,#191248,#191249,
#191250,#191251,#191252,#191253,#191254,#191255,#191256,#191257,#191258,
#191259,#191260,#191261,#191262,#191263,#191264,#191265,#191266,#191267,
#191268,#191269,#191270,#191271,#191272,#191273,#191274,#191275,#191276,
#191277,#191278,#191279,#191280,#191281,#191282,#191283,#191284,#191285,
#191286,#191287,#191288,#191289,#191290,#191291,#191292,#191293,#191294,
#191295,#191296,#191297,#191298,#191299,#191300,#191301,#191302,#191303,
#191304,#191305,#191306,#191307,#191308,#191309,#191310,#191311,#191312,
#191313,#191314,#191315,#191316,#191317,#191318,#191319,#191320,#191321,
#191322,#191323,#191324,#191325,#191326,#191327,#191328,#191329,#191330,
#191331,#191332,#191333,#191334,#191335,#191336,#191337,#191338,#191339,
#191340,#191341,#191342,#191343,#191344,#191345,#191346,#191347,#191348,
#191349,#191350,#191351,#191352,#191353,#191354,#191355,#191356,#191357,
#191358,#191359,#191360,#191361),.UNSPECIFIED.,.F.,.F.,(4,2,2,2,2,2,2,2,
2,2,2,2,2,2,2,2,2,2,2,2,2,2,2,2,2,2,2,2,2,2,2,2,2,2,2,2,2,2,2,2,2,2,2,2,
2,2,2,2,2,2,2,2,2,2,2,2,2,2,2,2,2,2,2,2,2,2,2,2,2,2,2,2,2,2,2,2,2,2,2,2,
2,2,2,2,2,2,2,2,2,2,2,2,2,2,2,2,2,2,2,2,2,2,2,2,2,2,2,2,2,2,2,2,2,2,2,2,
4),(0.0750288866695304,0.0988476388128419,0.111888896017187,0.115416384720813,
0.117551062967879,0.119473010908271,0.121926095772893,0.125833939336574,
0.147507513631184,0.207360988300454,0.215841413740865,0.219420342090852,
0.22135444545707,0.222628435301558,0.223822876379554,0.22486635864107,0.226245269920354,
0.22911009984437,0.264693456090149,0.297552629213783,0.320303169519504,
0.325982681899396,0.328558619925288,0.330497701947557,0.332322887219393,
0.334859323854595,0.341466097082073,0.397637306257989,0.421485895038357,
0.432250515347694,0.434490879017361,0.435740299795249,0.436812297051355,
0.438169343668719,0.440834379545483,0.458016218533738,0.507006516340784,
0.525230085590314,0.536276560196135,0.539607032913761,0.541698357521891,
0.543632406986323,0.546131673348657,0.550283003557895,0.578438583117287,
0.620515650582936,0.636279916483226,0.644544869789676,0.646608143657294,
0.647818540634769,0.648896890235033,0.650291652681477,0.652615888696389,
0.667025439902318,0.675569301872245,0.688665470740753,0.72151875655042,
0.744257070647802,0.749935208688195,0.75251105545168,0.754450284425893,
0.756275766114474,0.758812867790212,0.76542285705599,0.821575709471048,
0.845442611629954,0.856212653187838,0.858453513296996,0.859703121951681,
0.860775225443443,0.862132335981215,0.864797285493635,0.881970973850752,
0.92747365336257,0.955334410640888,0.961667095567586,0.964358854716377,
0.966317678344622,0.96811417670787,0.9709995618696,0.978006588705994,1.02934961057856,
1.05652184770716,1.06814571862572,1.07043634817434,1.07169680274305,1.0727679731605,
1.07411090498551,1.07670977558034,1.09222289794396,1.09879767692896,1.14018127845367,
1.16744975409078,1.17371040001649,1.17638989112832,1.17834659733112,1.18014589609658,
1.1830462493864,1.19014267214712,1.23977806686569,1.27816003863628,1.28174636449284,
1.28325749256897,1.28435012413588,1.28537564856719,1.28711628136227,1.29183188796299,
1.33224679737648,1.3341364500098,1.37796729601687,1.38519019214418,1.38811181430934,
1.38991506778615,1.39186881359856,1.39453121204554,1.40069275473419,1.40863554629314),
 .UNSPECIFIED.);
#1958=B_SPLINE_CURVE_WITH_KNOTS('',3,(#191367,#191368,#191369,#191370),
 .UNSPECIFIED.,.F.,.F.,(4,4),(152.105783788367,152.455231345441),
 .UNSPECIFIED.);
#1959=B_SPLINE_CURVE_WITH_KNOTS('',3,(#191371,#191372,#191373,#191374,#191375,
#191376,#191377,#191378,#191379,#191380,#191381,#191382,#191383,#191384,
#191385,#191386,#191387,#191388,#191389,#191390,#191391,#191392,#191393,
#191394,#191395,#191396,#191397,#191398,#191399,#191400,#191401,#191402,
#191403,#191404,#191405,#191406,#191407,#191408,#191409,#191410,#191411,
#191412,#191413,#191414,#191415,#191416,#191417,#191418,#191419,#191420,
#191421,#191422,#191423,#191424,#191425,#191426,#191427,#191428,#191429,
#191430,#191431,#191432,#191433,#191434,#191435,#191436,#191437,#191438,
#191439,#191440,#191441,#191442,#191443,#191444,#191445,#191446,#191447,
#191448,#191449,#191450,#191451,#191452,#191453,#191454,#191455,#191456,
#191457,#191458,#191459,#191460,#191461,#191462,#191463,#191464,#191465,
#191466,#191467,#191468,#191469,#191470,#191471,#191472,#191473,#191474,
#191475,#191476,#191477,#191478,#191479,#191480,#191481,#191482,#191483,
#191484,#191485,#191486,#191487,#191488,#191489,#191490,#191491,#191492,
#191493,#191494,#191495,#191496,#191497,#191498,#191499,#191500,#191501,
#191502,#191503,#191504,#191505,#191506,#191507,#191508,#191509,#191510,
#191511,#191512,#191513,#191514,#191515,#191516,#191517,#191518,#191519,
#191520,#191521,#191522,#191523,#191524,#191525,#191526,#191527,#191528,
#191529,#191530,#191531,#191532,#191533,#191534,#191535,#191536,#191537,
#191538,#191539,#191540,#191541,#191542,#191543,#191544,#191545,#191546,
#191547,#191548,#191549,#191550,#191551,#191552,#191553,#191554,#191555,
#191556,#191557,#191558,#191559,#191560,#191561,#191562,#191563,#191564,
#191565,#191566,#191567,#191568,#191569,#191570,#191571,#191572,#191573,
#191574,#191575,#191576,#191577,#191578,#191579,#191580,#191581,#191582,
#191583,#191584,#191585,#191586,#191587,#191588),.UNSPECIFIED.,.F.,.F.,
(4,2,2,2,2,2,2,2,2,2,2,2,2,2,2,2,2,2,2,2,2,2,2,2,2,2,2,2,2,2,2,2,2,2,2,
2,2,2,2,2,2,2,2,2,2,2,2,2,2,2,2,2,2,2,2,2,2,2,2,2,2,2,2,2,2,2,2,2,2,2,2,
2,2,2,2,2,2,2,2,2,2,2,2,2,2,2,2,2,2,2,2,2,2,2,2,2,2,2,2,2,2,2,2,2,2,2,2,
2,4),(0.000629330332896467,0.0481836283120002,0.0539124780237477,0.05787733475668,
0.0594504871787808,0.0605543059052947,0.0615643737818521,0.0632261135679029,
0.0674397512461144,0.117074899313782,0.145099746889406,0.159868702049087,
0.163472396047961,0.165305888284628,0.167218128087233,0.169427168350128,
0.173190872934244,0.187528077164309,0.194033219199103,0.231119072317868,
0.257108362976473,0.268435364721626,0.270708846750274,0.271965401439233,
0.273036609959852,0.274383853772958,0.277003561627561,0.293016737546607,
0.298054532289369,0.342300494321789,0.361132349055645,0.368618138341636,
0.374241455022956,0.376807011926189,0.378744445959156,0.380572619411744,
0.383120504417729,0.389800695683808,0.445225322817334,0.469564715247018,
0.480461488353643,0.482709803765115,0.483960932279112,0.485032715746576,
0.486387339952193,0.489041178184703,0.505923813355234,0.551390667602991,
0.582460329300252,0.586913729254806,0.589249257675527,0.591161254183334,
0.59337518483369,0.597159812813965,0.611728909326192,0.624007001074787,
0.664457786380243,0.683309566177892,0.692606095844698,0.69474884985209,
0.695976816916883,0.697051631759554,0.698440150294487,0.701354043952059,
0.731367395207987,0.782632281234815,0.791458724027022,0.79786005323276,
0.800563206648733,0.802523831735161,0.804317502987526,0.807188554083247,
0.814110550750721,0.86671263000008,0.892978558835595,0.904375992282532,
0.90665361251085,0.907911118757985,0.908982329221137,0.910328546421638,
0.912943237382301,0.928861144804925,0.929632069519631,0.973925248757589,
1.00329166350919,1.00980364292021,1.01252549468196,1.01448959719813,1.01627954387186,
1.01912967772102,1.02592428305164,1.0801280585937,1.10528993829633,1.1164042778108,
1.11866560919824,1.1199196132617,1.1209911875743,1.12234213348133,1.12497862061388,
1.14140772532225,1.19199097466867,1.20970069163456,1.22052321544298,1.22382937322598,
1.22591534971842,1.2278512719421,1.23036259075949,1.23455502155928,1.25961098705092),
 .UNSPECIFIED.);
#1960=B_SPLINE_CURVE_WITH_KNOTS('',3,(#191590,#191591,#191592,#191593,#191594,
#191595,#191596,#191597,#191598,#191599,#191600,#191601,#191602,#191603,
#191604,#191605,#191606,#191607,#191608,#191609,#191610,#191611,#191612,
#191613,#191614,#191615,#191616,#191617,#191618,#191619,#191620,#191621,
#191622,#191623,#191624,#191625,#191626,#191627,#191628,#191629,#191630,
#191631,#191632,#191633,#191634,#191635,#191636,#191637,#191638,#191639,
#191640,#191641,#191642,#191643,#191644,#191645,#191646,#191647,#191648,
#191649,#191650,#191651,#191652,#191653,#191654,#191655,#191656,#191657,
#191658,#191659,#191660,#191661,#191662,#191663,#191664,#191665,#191666,
#191667,#191668,#191669,#191670,#191671,#191672,#191673,#191674,#191675,
#191676,#191677,#191678,#191679,#191680,#191681,#191682,#191683,#191684,
#191685,#191686,#191687,#191688,#191689,#191690,#191691,#191692,#191693,
#191694,#191695,#191696,#191697,#191698,#191699,#191700,#191701,#191702,
#191703,#191704,#191705,#191706,#191707,#191708,#191709,#191710,#191711,
#191712,#191713,#191714,#191715,#191716,#191717,#191718,#191719,#191720,
#191721,#191722,#191723,#191724,#191725,#191726,#191727,#191728,#191729,
#191730,#191731,#191732,#191733,#191734,#191735,#191736,#191737,#191738,
#191739,#191740,#191741,#191742,#191743,#191744,#191745,#191746,#191747,
#191748,#191749,#191750,#191751,#191752,#191753,#191754,#191755,#191756,
#191757,#191758,#191759,#191760,#191761,#191762,#191763,#191764,#191765,
#191766,#191767,#191768,#191769,#191770,#191771,#191772,#191773,#191774,
#191775,#191776,#191777,#191778,#191779,#191780,#191781,#191782,#191783,
#191784,#191785,#191786,#191787,#191788,#191789,#191790,#191791,#191792,
#191793,#191794,#191795,#191796,#191797,#191798,#191799,#191800,#191801,
#191802,#191803,#191804,#191805,#191806,#191807,#191808,#191809),
 .UNSPECIFIED.,.F.,.F.,(4,2,2,2,2,2,2,2,2,2,2,2,2,2,2,2,2,2,2,2,2,2,2,2,
2,2,2,2,2,2,2,2,2,2,2,2,2,2,2,2,2,2,2,2,2,2,2,2,2,2,2,2,2,2,2,2,2,2,2,2,
2,2,2,2,2,2,2,2,2,2,2,2,2,2,2,2,2,2,2,2,2,2,2,2,2,2,2,2,2,2,2,2,2,2,2,2,
2,2,2,2,2,2,2,2,2,2,2,2,2,4),(1.40863554629314,1.42716215159709,1.46608335485054,
1.4742262937387,1.49150273493638,1.49417163629359,1.49552963938261,1.49660186907406,
1.49785096673155,1.50008926127109,1.51081615469342,1.53452084178693,1.56189720077975,
1.59383344740408,1.59807355130827,1.60059904422423,1.60253750501244,1.60461798644391,
1.60789797868523,1.61848080760563,1.6356493146767,1.68138674762876,1.68817256117372,
1.70360944883121,1.7059772390797,1.70738488073162,1.70846516546746,1.70966886176828,
1.71170129041267,1.71959671810318,1.73432520447475,1.76335930174742,1.80574607868969,
1.81003972128601,1.81258079153819,1.81452179636653,1.81659585752303,1.81984654089242,
1.83017072034651,1.84676248796964,1.8796785532681,1.89569119122154,1.89935457602018,
1.91554186909053,1.9181691129569,1.9195181936139,1.92058979219937,1.9218455709776,
1.92411450987405,1.93535545373384,1.96100072805648,2.01447068945007,2.02132576778302,
2.02418616726865,2.02597816979551,2.02794099109555,2.03065454626968,2.03711548181607,
2.09104317996443,2.12731082282962,2.13016509347575,2.1315421696298,2.13261606659975,
2.13385194986308,2.1360298053932,2.14582124223785,2.19471609134631,2.22983738282057,
2.23412739389796,2.23666735477647,2.23860811162243,2.24068248949139,2.24393488508621,
2.25427477893621,2.27090160239157,2.30384594427632,2.32163773658148,2.3395210915158,
2.34221127405255,2.34357378887543,2.34464634307932,2.3458921140461,2.3481152904112,
2.35859967555724,2.38142776393167,2.41099672670033,2.44190937607125,2.44650855264558,
2.44892542349954,2.45079410007683,2.4528901947448,2.45508756247662,2.4583380477175,
2.49660981719125,2.53859758144543,2.55185006429499,2.55411817912451,2.55549653647139,
2.55657299018092,2.55779346303841,2.55990153224842,2.56872789661443,2.58612906951568,
2.64880086677163,2.65696471589238,2.66003632479818,2.66186784621627,2.66371202387013,
2.66600413821752,2.66806871862646),.UNSPECIFIED.);
#1961=B_SPLINE_CURVE_WITH_KNOTS('',3,(#191810,#191811,#191812,#191813,#191814,
#191815,#191816,#191817,#191818,#191819),.UNSPECIFIED.,.F.,.F.,(4,2,2,2,
4),(0.000823833599433129,0.00391834426972108,0.0101607531916337,0.0637296745559499,
0.07512477121657),.UNSPECIFIED.);
#1962=B_SPLINE_CURVE_WITH_KNOTS('',3,(#191825,#191826,#191827,#191828,#191829,
#191830),.UNSPECIFIED.,.F.,.F.,(4,2,4),(2.59315591655363,2.60891629140922,
2.66742166236768),.UNSPECIFIED.);
#1963=B_SPLINE_CURVE_WITH_KNOTS('',3,(#191831,#191832,#191833,#191834,#191835,
#191836,#191837,#191838,#191839,#191840),.UNSPECIFIED.,.F.,.F.,(4,1,1,1,
1,1,1,4),(152.455231345441,152.821976844167,153.820813294129,154.81964974409,
155.818486194052,156.817322644014,157.816159093976,158.388969095546),
 .UNSPECIFIED.);
#1964=B_SPLINE_CURVE_WITH_KNOTS('',3,(#191841,#191842,#191843,#191844,#191845,
#191846,#191847,#191848,#191849,#191850,#191851,#191852,#191853,#191854,
#191855,#191856,#191857,#191858,#191859,#191860,#191861,#191862,#191863,
#191864,#191865,#191866,#191867,#191868,#191869,#191870,#191871,#191872,
#191873,#191874,#191875,#191876,#191877,#191878,#191879,#191880,#191881,
#191882,#191883,#191884,#191885,#191886,#191887,#191888,#191889,#191890,
#191891,#191892,#191893,#191894,#191895,#191896,#191897,#191898,#191899,
#191900,#191901,#191902,#191903,#191904,#191905,#191906,#191907,#191908,
#191909,#191910,#191911,#191912,#191913,#191914,#191915,#191916,#191917,
#191918,#191919,#191920,#191921,#191922,#191923,#191924,#191925,#191926,
#191927,#191928,#191929,#191930,#191931,#191932,#191933,#191934,#191935,
#191936,#191937,#191938,#191939,#191940,#191941,#191942,#191943,#191944,
#191945,#191946,#191947,#191948,#191949,#191950,#191951,#191952,#191953,
#191954,#191955,#191956,#191957,#191958,#191959,#191960,#191961,#191962,
#191963,#191964,#191965,#191966,#191967,#191968,#191969,#191970,#191971,
#191972,#191973,#191974,#191975,#191976,#191977,#191978,#191979,#191980,
#191981,#191982,#191983,#191984,#191985,#191986,#191987,#191988,#191989,
#191990,#191991,#191992,#191993,#191994,#191995,#191996,#191997,#191998,
#191999,#192000,#192001,#192002,#192003,#192004,#192005,#192006,#192007,
#192008,#192009,#192010,#192011,#192012,#192013,#192014,#192015,#192016,
#192017,#192018,#192019,#192020,#192021,#192022,#192023,#192024,#192025,
#192026,#192027,#192028,#192029,#192030,#192031,#192032,#192033,#192034,
#192035,#192036,#192037,#192038,#192039,#192040,#192041,#192042,#192043,
#192044,#192045,#192046,#192047,#192048,#192049,#192050,#192051,#192052,
#192053,#192054,#192055,#192056,#192057,#192058,#192059,#192060,#192061,
#192062,#192063,#192064,#192065,#192066,#192067,#192068,#192069,#192070,
#192071,#192072,#192073,#192074),.UNSPECIFIED.,.F.,.F.,(4,2,2,2,2,2,2,2,
2,2,2,2,2,2,2,2,2,2,2,2,2,2,2,2,2,2,2,2,2,2,2,2,2,2,2,2,2,2,2,2,2,2,2,2,
2,2,2,2,2,2,2,2,2,2,2,2,2,2,2,2,2,2,2,2,2,2,2,2,2,2,2,2,2,2,2,2,2,2,2,2,
2,2,2,2,2,2,2,2,2,2,2,2,2,2,2,2,2,2,2,2,2,2,2,2,2,2,2,2,2,2,2,2,2,2,2,2,
4),(0.07512477121657,0.0866656614041577,0.0971787061917909,0.0994034139875145,
0.100649374983133,0.101721680739751,0.103083340651343,0.105770202884318,
0.123569836670099,0.183744945029975,0.200301942100647,0.203058816148262,
0.205554098781904,0.207453881261889,0.209279756454386,0.211819138400779,
0.218445141181668,0.274398200532703,0.298387415254804,0.309189818023144,
0.311432362033971,0.312682200516078,0.313754063516151,0.315110307992711,
0.317771871894378,0.334863658205109,0.380432706677751,0.408296195764049,
0.414628676252824,0.417320108936067,0.419278606857167,0.42107474541533,
0.423959418499773,0.430964032001749,0.48232321654618,0.509471790058244,
0.521088952724782,0.523378911923478,0.524639083027632,0.525710063956928,
0.527052823367524,0.52965154984707,0.545169501854001,0.592242170237513,
0.620259136846318,0.626610255077,0.629304907007226,0.631264021391924,0.633059530301395,
0.635940570563124,0.642922975181822,0.694639667019797,0.721533832947211,
0.733088375071281,0.735374885605499,0.736634330149682,0.737705399270661,
0.739049164328244,0.741652445975924,0.757275925677643,0.775418506847907,
0.777790870533834,0.810581386111433,0.833222084705453,0.838886993974625,
0.841460381041518,0.843399196152501,0.845225343494201,0.847765061428206,
0.854391825377458,0.910379596898951,0.934353181570827,0.945152042035031,
0.947394622720328,0.948644590082684,0.949716630493261,0.951073185283515,
0.95322029269039,0.964281235493402,1.01542252771507,1.04414436575984,1.05058033864303,
1.05328955602246,1.05525147030904,1.05704418198381,1.05990904150288,1.06679202178475,
1.11993302602103,1.1458307050905,1.15713530015814,1.15940781889123,1.16066431652466,
1.16173576521977,1.16308367872507,1.16570576983221,1.18175217783023,1.18586394160893,
1.20155431469556,1.23444009412102,1.25722651025384,1.26291138423872,1.26548861519639,
1.26742820930306,1.26925353863326,1.27178963464469,1.27839235753856,1.33462642983714,
1.35357799982722,1.36857940875808,1.37092931106035,1.37233171707441,1.37341125657246,
1.37461775534265,1.37666285255934,1.38470692584711,1.39984630235978,1.40873796955923),
 .UNSPECIFIED.);
#1965=B_SPLINE_CURVE_WITH_KNOTS('',3,(#192079,#192080,#192081,#192082,#192083,
#192084,#192085,#192086,#192087,#192088,#192089,#192090,#192091,#192092,
#192093,#192094,#192095,#192096,#192097,#192098,#192099,#192100,#192101,
#192102,#192103,#192104,#192105,#192106,#192107,#192108,#192109,#192110,
#192111,#192112,#192113,#192114,#192115,#192116,#192117,#192118,#192119,
#192120,#192121,#192122,#192123,#192124,#192125,#192126,#192127,#192128,
#192129,#192130,#192131,#192132,#192133,#192134,#192135,#192136,#192137,
#192138,#192139,#192140,#192141,#192142,#192143,#192144,#192145,#192146,
#192147,#192148,#192149,#192150,#192151,#192152,#192153,#192154,#192155,
#192156,#192157,#192158,#192159,#192160,#192161,#192162,#192163,#192164,
#192165,#192166,#192167,#192168,#192169,#192170,#192171,#192172,#192173,
#192174,#192175,#192176,#192177,#192178,#192179,#192180,#192181,#192182,
#192183,#192184,#192185,#192186,#192187,#192188,#192189,#192190,#192191,
#192192,#192193,#192194,#192195,#192196,#192197,#192198,#192199,#192200,
#192201,#192202,#192203,#192204,#192205,#192206,#192207,#192208,#192209,
#192210,#192211,#192212,#192213,#192214,#192215,#192216,#192217,#192218,
#192219,#192220,#192221,#192222,#192223,#192224,#192225,#192226,#192227,
#192228,#192229,#192230,#192231,#192232,#192233,#192234,#192235,#192236,
#192237,#192238,#192239,#192240,#192241,#192242,#192243,#192244,#192245,
#192246,#192247,#192248,#192249,#192250,#192251,#192252,#192253,#192254,
#192255,#192256,#192257,#192258,#192259,#192260,#192261,#192262,#192263,
#192264,#192265,#192266,#192267,#192268,#192269,#192270,#192271,#192272,
#192273,#192274,#192275,#192276,#192277,#192278,#192279,#192280,#192281,
#192282,#192283,#192284,#192285,#192286,#192287,#192288,#192289,#192290,
#192291,#192292,#192293,#192294,#192295,#192296,#192297,#192298,#192299,
#192300,#192301,#192302,#192303,#192304,#192305,#192306,#192307,#192308,
#192309,#192310,#192311,#192312),.UNSPECIFIED.,.F.,.F.,(4,2,2,2,2,2,2,2,
2,2,2,2,2,2,2,2,2,2,2,2,2,2,2,2,2,2,2,2,2,2,2,2,2,2,2,2,2,2,2,2,2,2,2,2,
2,2,2,2,2,2,2,2,2,2,2,2,2,2,2,2,2,2,2,2,2,2,2,2,2,2,2,2,2,2,2,2,2,2,2,2,
2,2,2,2,2,2,2,2,2,2,2,2,2,2,2,2,2,2,2,2,2,2,2,2,2,2,2,2,2,2,2,2,2,2,2,2,
4),(1.25960928709908,1.26784055573431,1.2907030527357,1.30119586065487,
1.3034192843059,1.3046649539869,1.30573723567159,1.3070991650138,1.30978755149372,
1.32763515531548,1.33373204709831,1.37574263222815,1.40292854225494,1.40705404575204,
1.4095456068141,1.41147833486376,1.41357286154704,1.41691845643489,1.42810816287076,
1.44666703949846,1.49069764380321,1.49656852631586,1.51244824860124,1.51506158847437,
1.51640744979989,1.51747862301405,1.51873640744419,1.52101504583588,1.53242880949112,
1.55875577111714,1.61123416629037,1.6181633430875,1.62103576667108,1.62282983176323,
1.62479052237024,1.62749309201263,1.63388985990958,1.68178083519589,1.72137474943336,
1.72610770227625,1.7278508967438,1.72887687896778,1.72996904592675,1.73147807218518,
1.73505282026033,1.77424775366377,1.82298113051944,1.83011227083648,1.83301820045556,
1.83481835059661,1.83677392681743,1.83944815625023,1.84567949843769,1.87271609449124,
1.91342988717374,1.93614233522075,1.93899617344875,1.9403730023126,1.94144668744679,
1.94268230334877,1.94485963231244,1.95464777071552,2.00353402176072,2.0386407217033,
2.04293541856535,2.04547648054644,2.04741711461237,2.0494904259782,2.05273919523384,
2.06305105273228,2.07961704929546,2.11250729383114,2.12706552683484,2.13238544468093,
2.14842388940541,2.15104513914485,2.15239273955484,2.15346401037507,2.15472039190784,
2.156992886137,2.1683017030916,2.19421613130566,2.24727727988239,2.25416193182608,
2.25702681904081,2.25881935758839,2.26078093521539,2.2634894100444,2.26992228791662,
2.29862561082173,2.34984929424604,2.36088140272063,2.36302660706477,2.36438250817935,
2.36545439847882,2.3667046166138,2.36894871961712,2.37977592854959,2.40385355560873,
2.45963351474795,2.46627478844487,2.46881661701892,2.47064319794461,2.47251919219428,
2.47500298951852,2.47774055588461,2.4822908937083,2.49161776582798,2.54225892254908,
2.57203619480185,2.57495056673749,2.57633918006039,2.57741400341707,2.57864191699185,
2.58078441361074,2.59007759676306,2.59315591655363),.UNSPECIFIED.);
#1966=B_SPLINE_CURVE_WITH_KNOTS('',3,(#192314,#192315,#192316,#192317,#192318,
#192319,#192320,#192321,#192322,#192323,#192324,#192325,#192326,#192327,
#192328,#192329,#192330,#192331,#192332,#192333,#192334,#192335,#192336,
#192337,#192338,#192339,#192340,#192341,#192342,#192343,#192344,#192345,
#192346,#192347,#192348,#192349,#192350,#192351,#192352,#192353,#192354,
#192355,#192356,#192357,#192358,#192359,#192360,#192361,#192362,#192363,
#192364,#192365,#192366,#192367,#192368,#192369,#192370,#192371,#192372,
#192373,#192374,#192375,#192376,#192377,#192378,#192379,#192380,#192381,
#192382,#192383,#192384,#192385,#192386,#192387,#192388,#192389,#192390,
#192391,#192392,#192393,#192394,#192395,#192396,#192397,#192398,#192399,
#192400,#192401,#192402,#192403,#192404,#192405,#192406,#192407,#192408,
#192409,#192410,#192411,#192412,#192413,#192414,#192415,#192416,#192417,
#192418,#192419,#192420,#192421,#192422,#192423,#192424,#192425,#192426,
#192427,#192428,#192429,#192430,#192431,#192432,#192433,#192434,#192435,
#192436,#192437,#192438,#192439,#192440,#192441,#192442,#192443,#192444,
#192445,#192446,#192447,#192448,#192449,#192450,#192451,#192452,#192453,
#192454,#192455,#192456,#192457,#192458,#192459,#192460,#192461,#192462,
#192463,#192464,#192465,#192466,#192467,#192468,#192469,#192470,#192471,
#192472,#192473,#192474,#192475,#192476,#192477,#192478,#192479,#192480,
#192481,#192482,#192483,#192484,#192485,#192486,#192487,#192488,#192489,
#192490,#192491,#192492,#192493,#192494,#192495,#192496,#192497,#192498,
#192499,#192500,#192501,#192502,#192503,#192504,#192505,#192506,#192507,
#192508,#192509,#192510,#192511,#192512,#192513,#192514,#192515,#192516,
#192517,#192518,#192519,#192520,#192521,#192522,#192523,#192524,#192525,
#192526,#192527,#192528,#192529,#192530,#192531,#192532,#192533,#192534,
#192535,#192536,#192537,#192538,#192539,#192540,#192541),.UNSPECIFIED.,
 .F.,.F.,(4,2,2,2,2,2,2,2,2,2,2,2,2,2,2,2,2,2,2,2,2,2,2,2,2,2,2,2,2,2,2,
2,2,2,2,2,2,2,2,2,2,2,2,2,2,2,2,2,2,2,2,2,2,2,2,2,2,2,2,2,2,2,2,2,2,2,2,
2,2,2,2,2,2,2,2,2,2,2,2,2,2,2,2,2,2,2,2,2,2,2,2,2,2,2,2,2,2,2,2,2,2,2,2,
2,2,2,2,2,2,2,2,2,2,4),(1.40873796955923,1.43954407347186,1.47079848867483,
1.4750246618546,1.47754608919005,1.47948389600165,1.48156609514269,1.48485392083813,
1.49550691464887,1.51283341063729,1.55311673063461,1.58010788384515,1.58301000885525,
1.58439643279473,1.58547124458416,1.58670103017614,1.58885122205798,1.59824667699909,
1.64748097300911,1.68269695329597,1.68699377340832,1.68953569495947,1.69147675734442,
1.69355030532848,1.69679898444777,1.70710668012022,1.7236623322147,1.75654736158497,
1.77010034868505,1.7774148449482,1.78177139990558,1.79293656332903,1.79509015725136,
1.79644870944042,1.79752093565588,1.79876952824895,1.80100566978832,1.811698694541,
1.83528019688316,1.89183149432246,1.89839602867847,1.90092591023938,1.90274951167987,
1.90468980742426,1.90727230391559,1.91298661612148,1.93599639997058,1.96905175821786,
1.99032132737911,2.00463237470267,2.00695314822479,2.0083469093453,2.00942514706726,
2.01063616926891,2.01270216615563,2.02100007169377,2.03685582517001,2.07906214793458,
2.10693287600035,2.11107655852846,2.11357363721655,2.11550741321349,2.11759985474868,
2.12093515510041,2.1320257106873,2.15035357269575,2.19838987285337,2.21636746232778,
2.21906065773651,2.22042375214956,2.22149627852515,2.22274146334813,2.22496223156422,
2.23541039286213,2.25811056621867,2.31604731638538,2.32244996429073,2.32495328846761,
2.32676986813482,2.32871401257197,2.33132120656349,2.33717234850553,2.36121619394524,
2.39060946057178,2.42822159314567,2.43104799992162,2.43241941944457,2.43349260124657,
2.43470695411841,2.43681596775364,2.43942266769537,2.44486047009304,2.46039785712345,
2.5018936809362,2.51079094849619,2.51723003235368,2.5321772650075,2.5359953013133,
2.5382170021158,2.5401286335118,2.54245486592691,2.54686349993011,2.57633055051127,
2.61936098785009,2.62769189673351,2.64069601077808,2.6429513496057,2.64434060170266,
2.64541553558637,2.64642425852135,2.6476373153628,2.64942356192591,2.65515826803913,
2.66782561093684),.UNSPECIFIED.);
#1967=B_SPLINE_CURVE_WITH_KNOTS('',3,(#192542,#192543,#192544,#192545,#192546,
#192547,#192548,#192549,#192550,#192551,#192552,#192553,#192554),
 .UNSPECIFIED.,.F.,.F.,(4,3,3,3,4),(-161.271232351587,-161.169466141419,
-161.067655433098,-160.96569395549,-160.920671713183),.UNSPECIFIED.);
#1968=B_SPLINE_CURVE_WITH_KNOTS('',3,(#192560,#192561,#192562,#192563,#192564,
#192565,#192566,#192567,#192568,#192569,#192570,#192571,#192572),
 .UNSPECIFIED.,.F.,.F.,(4,3,3,3,4),(170.955339710339,171.057208844183,171.158971096373,
171.260660134248,171.305836553012),.UNSPECIFIED.);
#1969=B_SPLINE_CURVE_WITH_KNOTS('',3,(#192573,#192574,#192575,#192576,#192577,
#192578,#192579,#192580,#192581,#192582,#192583,#192584,#192585,#192586,
#192587,#192588,#192589,#192590,#192591,#192592,#192593,#192594,#192595,
#192596,#192597,#192598,#192599,#192600,#192601,#192602,#192603,#192604,
#192605,#192606,#192607,#192608,#192609,#192610,#192611,#192612,#192613,
#192614,#192615,#192616,#192617,#192618,#192619,#192620,#192621,#192622,
#192623,#192624,#192625,#192626,#192627,#192628,#192629,#192630,#192631,
#192632,#192633,#192634,#192635,#192636,#192637,#192638,#192639,#192640,
#192641,#192642,#192643,#192644,#192645,#192646,#192647,#192648,#192649,
#192650,#192651,#192652,#192653,#192654,#192655,#192656,#192657,#192658,
#192659,#192660,#192661,#192662,#192663,#192664,#192665,#192666,#192667,
#192668,#192669,#192670,#192671,#192672,#192673,#192674,#192675,#192676,
#192677,#192678,#192679,#192680,#192681,#192682,#192683,#192684,#192685,
#192686,#192687,#192688,#192689,#192690,#192691,#192692,#192693,#192694,
#192695,#192696,#192697,#192698,#192699,#192700,#192701,#192702,#192703,
#192704,#192705,#192706,#192707,#192708,#192709,#192710,#192711,#192712,
#192713,#192714,#192715,#192716,#192717,#192718,#192719,#192720,#192721,
#192722,#192723,#192724,#192725,#192726,#192727,#192728,#192729,#192730,
#192731,#192732,#192733,#192734,#192735,#192736,#192737,#192738,#192739,
#192740,#192741,#192742,#192743,#192744,#192745,#192746,#192747,#192748,
#192749,#192750,#192751,#192752,#192753,#192754,#192755,#192756,#192757,
#192758,#192759,#192760,#192761,#192762,#192763,#192764,#192765,#192766,
#192767,#192768,#192769,#192770,#192771,#192772,#192773,#192774,#192775,
#192776,#192777,#192778,#192779,#192780,#192781,#192782,#192783,#192784,
#192785,#192786,#192787,#192788,#192789,#192790,#192791,#192792,#192793,
#192794),.UNSPECIFIED.,.F.,.F.,(4,2,2,2,2,2,2,2,2,2,2,2,2,2,2,2,2,2,2,2,
2,2,2,2,2,2,2,2,2,2,2,2,2,2,2,2,2,2,2,2,2,2,2,2,2,2,2,2,2,2,2,2,2,2,2,2,
2,2,2,2,2,2,2,2,2,2,2,2,2,2,2,2,2,2,2,2,2,2,2,2,2,2,2,2,2,2,2,2,2,2,2,2,
2,2,2,2,2,2,2,2,2,2,2,2,2,2,2,2,2,2,4),(0.000655551428707671,0.0215327131636358,
0.0285521200326831,0.0303960837974268,0.0316335735611994,0.032648445331859,
0.0337175330357083,0.035063454125746,0.0377856382359734,0.0559587373523061,
0.0616380686718176,0.0739377203228541,0.0845184170710276,0.106384424938896,
0.12297703761806,0.133286020145618,0.136520189199687,0.138580633014089,
0.140506643026182,0.143024716935975,0.147271544853911,0.192337496499189,
0.220917475857183,0.234450932701798,0.241868965911147,0.243841365085469,
0.244851087594292,0.245918126759799,0.247244742074754,0.249294071989488,
0.258883054629126,0.318505517323277,0.335297050192059,0.345718697613677,
0.348984721134232,0.351065006938216,0.353009378570062,0.355551374960315,
0.359839085161449,0.394233154429761,0.443435840109631,0.453287245382845,
0.455474802171122,0.456715771455664,0.457792036134616,0.459170705228411,
0.462028639566066,0.48480767131069,0.527329099661624,0.545904425390008,
0.55710221315087,0.560449734769267,0.562545400708846,0.564479142195401,
0.56697196403246,0.571099480905268,0.598277944722438,0.640347082526372,
0.656907907771879,0.66544954843179,0.667534893846574,0.668750026935094,
0.66982647738543,0.671211207856338,0.673503592060509,0.687287341627991,
0.698620516742917,0.737949645182713,0.764492288535883,0.770660358832987,
0.773322000804491,0.775273825915658,0.777074342259877,0.779989342853213,
0.787184837110465,0.833863301118626,0.856213723393924,0.870037628643727,
0.875062763886551,0.878645291653255,0.880154587653599,0.881246023642936,
0.882271307705382,0.884011280405899,0.888723629530098,0.929074828428406,
0.977358980984542,0.982966721211285,0.985529978576998,0.98746765419356,
0.989297520405304,0.991850133235058,0.998557316842197,1.05366063683498,
1.07817671190707,1.08912119333522,1.09137329019702,1.09262570653631,1.09369780718571,
1.09505199671401,1.09779133798081,1.11614975276579,1.16514969504523,1.18898303750825,
1.19480676010273,1.19740896677571,1.1993522579715,1.20117011609438,1.20367847747491,
1.21011174770897,1.25960928709908),.UNSPECIFIED.);
#1970=B_SPLINE_CURVE_WITH_KNOTS('',3,(#192796,#192797,#192798,#192799,#192800,
#192801,#192802,#192803,#192804,#192805,#192806,#192807,#192808,#192809,
#192810,#192811,#192812,#192813,#192814,#192815,#192816,#192817,#192818,
#192819,#192820,#192821,#192822,#192823,#192824,#192825,#192826,#192827,
#192828,#192829,#192830,#192831,#192832,#192833,#192834,#192835,#192836,
#192837,#192838,#192839,#192840,#192841,#192842,#192843,#192844,#192845,
#192846,#192847,#192848,#192849,#192850,#192851,#192852,#192853,#192854,
#192855,#192856,#192857,#192858,#192859,#192860,#192861,#192862,#192863,
#192864,#192865,#192866,#192867,#192868,#192869,#192870,#192871,#192872,
#192873,#192874,#192875,#192876,#192877,#192878,#192879,#192880,#192881,
#192882,#192883,#192884,#192885,#192886,#192887,#192888,#192889,#192890,
#192891,#192892,#192893,#192894,#192895,#192896,#192897,#192898,#192899,
#192900,#192901,#192902,#192903,#192904,#192905,#192906,#192907,#192908,
#192909,#192910,#192911,#192912,#192913,#192914,#192915,#192916,#192917,
#192918,#192919,#192920,#192921,#192922,#192923,#192924,#192925,#192926,
#192927,#192928,#192929,#192930,#192931,#192932,#192933,#192934,#192935,
#192936,#192937,#192938,#192939,#192940,#192941,#192942,#192943,#192944,
#192945,#192946,#192947,#192948,#192949,#192950,#192951,#192952,#192953,
#192954,#192955,#192956,#192957,#192958,#192959,#192960,#192961,#192962,
#192963,#192964,#192965,#192966,#192967,#192968,#192969,#192970,#192971,
#192972,#192973,#192974,#192975,#192976),.UNSPECIFIED.,.F.,.F.,(4,3,3,3,
3,3,3,3,3,3,3,3,3,3,3,3,3,3,3,3,3,3,3,3,3,3,3,3,3,3,3,3,3,3,3,3,3,3,3,3,
3,3,3,3,3,3,3,3,3,3,3,3,3,3,3,3,3,3,3,3,4),(-167.203857019737,-167.08981105619,
-166.975344513777,-166.860315157044,-166.805687143633,-166.702287413269,
-166.599041101161,-166.495916075704,-166.392856431583,-166.289828138948,
-166.186797211101,-166.083659393271,-165.98046526208,-165.877088303416,
-165.806850693671,-165.703453680563,-165.60021006525,-165.497087692404,
-165.394030672259,-165.291004971,-165.187976597935,-165.084841260237,-164.981649571235,
-164.878274965853,-164.808014243709,-164.704622130422,-164.601383514024,
-164.49826626414,-164.395214440686,-164.292194002343,-164.189170950985,
-164.086040989101,-163.982854714538,-163.879485526039,-163.809177793747,
-163.705782195491,-163.602540043973,-163.49941920119,-163.396363751132,
-163.293339657762,-163.190312928204,-163.087179277827,-162.983989303286,
-162.880616437379,-162.810341343785,-162.706946383757,-162.603704871958,
-162.500584667953,-162.397529855753,-162.294506398376,-162.191480301996,
-162.088347276007,-161.985157921902,-161.881785663091,-161.811504893824,
-161.70947172983,-161.607582180158,-161.505807287657,-161.404097849771,
-161.302405179864,-161.271232351587),.UNSPECIFIED.);
#1971=B_SPLINE_CURVE_WITH_KNOTS('',3,(#192977,#192978,#192979,#192980,#192981,
#192982,#192983,#192984,#192985,#192986,#192987,#192988,#192989),
 .UNSPECIFIED.,.F.,.F.,(4,3,3,3,4),(-167.553337646663,-167.448855727829,
-167.344457483332,-167.240110556711,-167.203857020092),.UNSPECIFIED.);
#1972=B_SPLINE_CURVE_WITH_KNOTS('',3,(#192995,#192996,#192997,#192998,#192999,
#193000,#193001,#193002,#193003,#193004),.UNSPECIFIED.,.F.,.F.,(4,3,3,4),
(7.59252172359161,7.70650209815482,7.82442144397709,7.94234078979936),
 .UNSPECIFIED.);
#1973=B_SPLINE_CURVE_WITH_KNOTS('',3,(#193006,#193007,#193008,#193009,#193010,
#193011,#193012,#193013,#193014,#193015,#193016,#193017,#193018,#193019,
#193020,#193021,#193022,#193023,#193024,#193025,#193026,#193027,#193028,
#193029,#193030,#193031,#193032,#193033,#193034,#193035,#193036,#193037,
#193038,#193039,#193040,#193041,#193042,#193043,#193044,#193045,#193046,
#193047,#193048,#193049,#193050,#193051,#193052,#193053,#193054,#193055,
#193056,#193057,#193058,#193059,#193060,#193061,#193062,#193063,#193064,
#193065,#193066,#193067,#193068,#193069,#193070,#193071,#193072,#193073,
#193074,#193075,#193076,#193077,#193078,#193079,#193080,#193081,#193082,
#193083,#193084,#193085,#193086,#193087,#193088,#193089,#193090,#193091,
#193092,#193093,#193094,#193095,#193096,#193097,#193098,#193099,#193100,
#193101,#193102,#193103,#193104,#193105,#193106,#193107,#193108,#193109,
#193110,#193111,#193112,#193113,#193114,#193115,#193116,#193117,#193118,
#193119,#193120,#193121,#193122,#193123,#193124,#193125,#193126,#193127,
#193128,#193129,#193130,#193131,#193132,#193133,#193134,#193135,#193136,
#193137,#193138,#193139,#193140,#193141,#193142,#193143,#193144,#193145,
#193146,#193147,#193148,#193149,#193150,#193151,#193152,#193153,#193154,
#193155,#193156,#193157,#193158,#193159,#193160,#193161,#193162,#193163,
#193164,#193165,#193166,#193167,#193168,#193169,#193170,#193171,#193172,
#193173,#193174),.UNSPECIFIED.,.F.,.F.,(4,3,3,3,3,3,3,3,3,3,3,3,3,3,3,3,
3,3,3,3,3,3,3,3,3,3,3,3,3,3,3,3,3,3,3,3,3,3,3,3,3,3,3,3,3,3,3,3,3,3,3,3,
3,3,3,3,4),(2.00878451764821,2.11210391279692,2.21526989698117,2.31831446525096,
2.42129383098617,2.52424213980858,2.62719349431534,2.73024965054147,2.83336280284661,
2.93665222006101,2.99650934988563,3.10008230986109,3.20350557536163,3.30681224772116,
3.4100563283188,3.51327157245755,3.61649169494142,3.71982084946894,3.82320780718055,
3.92677785652903,3.99534579984751,4.09860812441835,4.2017150863826,4.30469852295217,
4.40761526975675,4.51049956061293,4.61338558491655,4.71637810302099,4.81942648355166,
4.92265858166643,4.99418224980938,5.09760358352983,5.20087156240154,5.30401824171002,
5.40709952008129,5.51014939511661,5.61320182122769,5.71636085636684,5.81957608032993,
5.92297369428319,5.99301869977126,6.09643423755244,6.19969678686738,6.30283861434793,
6.40591539958098,6.50896114779516,6.61200982139876,6.71516571129313,6.81837812515205,
6.9217735049757,6.99185514973314,7.0967069869202,7.20139081251388,7.30591389133753,
7.41034214208164,7.51471167951793,7.59252172323623),.UNSPECIFIED.);
#1974=B_SPLINE_CURVE_WITH_KNOTS('',3,(#193178,#193179,#193180,#193181,#193182,
#193183,#193184,#193185,#193186,#193187,#193188,#193189,#193190,#193191,
#193192,#193193,#193194,#193195,#193196,#193197,#193198,#193199,#193200,
#193201,#193202,#193203,#193204,#193205,#193206,#193207,#193208,#193209,
#193210,#193211,#193212,#193213,#193214,#193215,#193216,#193217,#193218,
#193219,#193220,#193221,#193222,#193223,#193224,#193225,#193226,#193227,
#193228,#193229,#193230,#193231,#193232,#193233,#193234,#193235,#193236,
#193237,#193238,#193239,#193240,#193241,#193242,#193243,#193244,#193245,
#193246,#193247,#193248,#193249,#193250,#193251,#193252,#193253,#193254,
#193255,#193256,#193257,#193258,#193259,#193260,#193261,#193262,#193263,
#193264,#193265,#193266,#193267,#193268,#193269,#193270,#193271,#193272,
#193273,#193274,#193275,#193276,#193277,#193278,#193279,#193280,#193281,
#193282,#193283,#193284,#193285,#193286,#193287,#193288,#193289,#193290,
#193291,#193292,#193293,#193294,#193295),.UNSPECIFIED.,.F.,.F.,(4,3,3,3,
3,3,3,3,3,3,3,3,3,3,3,3,3,3,3,3,3,3,3,3,3,3,3,3,3,3,3,3,3,3,3,3,3,3,3,4),
(-3.84103903298818,-3.73547282260036,-3.63371534451888,-3.53202565477874,
-3.43036802202408,-3.3287067634427,-3.22694496884903,-3.12512264837507,
-3.02313913493882,-2.99650934988562,-2.89298838415395,-2.7896184205715,
-2.68636679313977,-2.58317880759893,-2.48002064176421,-2.37685851496106,
-2.27358841489219,-2.17026119505925,-2.06675136672922,-1.99767289992375,
-1.89536901188924,-1.79321917542629,-1.69118674247093,-1.58921701577407,
-1.48727463022112,-1.3853242611676,-1.28325154596761,-1.18111583450438,
-1.07877443242794,-0.998836449961874,-0.892563151715309,-0.780992757750895,
-0.675072785964147,-0.569252409114428,-0.463503885892126,-0.357799564693429,
-0.252082102978388,-0.146359553840664,-0.0405640348441741,0.),
 .UNSPECIFIED.);
#1975=B_SPLINE_CURVE_WITH_KNOTS('',3,(#193296,#193297,#193298,#193299,#193300,
#193301,#193302,#193303,#193304,#193305,#193306,#193307,#193308,#193309,
#193310,#193311,#193312,#193313,#193314,#193315,#193316,#193317,#193318,
#193319,#193320,#193321),.UNSPECIFIED.,.F.,.F.,(4,2,2,2,2,2,2,2,2,2,2,2,
4),(0.000655554096865791,0.0215326957973204,0.028552110634771,0.0303960798049156,
0.0316335711042768,0.0326484421215227,0.0337175280396046,0.0350634423926314,
0.0377855980008208,0.0559579040604788,0.0616381299228464,0.0739378344818628,
0.0747573278913931),.UNSPECIFIED.);
#1976=B_SPLINE_CURVE_WITH_KNOTS('',3,(#193327,#193328,#193329,#193330,#193331,
#193332,#193333,#193334,#193335,#193336,#193337,#193338,#193339,#193340,
#193341,#193342,#193343,#193344,#193345,#193346,#193347,#193348,#193349,
#193350),.UNSPECIFIED.,.F.,.F.,(4,2,2,2,2,2,2,2,2,2,2,4),(2.59392175456229,
2.61962491033593,2.62795697204938,2.64096287978827,2.64321853041206,2.64460797466987,
2.64568305731841,2.64669191990705,2.64790514474502,2.64969163875382,2.65542713745129,
2.66809622952257),.UNSPECIFIED.);
#1977=B_SPLINE_CURVE_WITH_KNOTS('',3,(#193351,#193352,#193353,#193354,#193355,
#193356,#193357,#193358,#193359,#193360,#193361,#193362,#193363,#193364,
#193365,#193366,#193367,#193368,#193369,#193370,#193371,#193372,#193373,
#193374,#193375,#193376,#193377,#193378,#193379,#193380,#193381,#193382,
#193383,#193384,#193385,#193386,#193387,#193388,#193389,#193390,#193391,
#193392,#193393,#193394,#193395,#193396,#193397,#193398,#193399,#193400,
#193401,#193402,#193403,#193404,#193405,#193406,#193407,#193408,#193409,
#193410,#193411,#193412,#193413,#193414,#193415,#193416,#193417,#193418,
#193419,#193420,#193421,#193422,#193423,#193424,#193425,#193426,#193427,
#193428,#193429,#193430,#193431,#193432,#193433,#193434,#193435,#193436,
#193437,#193438,#193439,#193440,#193441,#193442,#193443,#193444,#193445,
#193446,#193447,#193448,#193449,#193450,#193451,#193452,#193453,#193454,
#193455,#193456,#193457,#193458,#193459,#193460,#193461,#193462,#193463,
#193464,#193465,#193466,#193467,#193468,#193469,#193470,#193471,#193472,
#193473,#193474,#193475,#193476,#193477,#193478,#193479,#193480,#193481,
#193482,#193483,#193484,#193485,#193486,#193487,#193488,#193489,#193490,
#193491,#193492,#193493,#193494,#193495,#193496,#193497,#193498,#193499,
#193500,#193501,#193502,#193503,#193504,#193505,#193506,#193507,#193508,
#193509,#193510,#193511,#193512,#193513,#193514,#193515,#193516,#193517,
#193518,#193519,#193520,#193521,#193522,#193523,#193524,#193525,#193526,
#193527,#193528,#193529,#193530,#193531),.UNSPECIFIED.,.F.,.F.,(4,3,3,3,
3,3,3,3,3,3,3,3,3,3,3,3,3,3,3,3,3,3,3,3,3,3,3,3,3,3,3,3,3,3,3,3,3,3,3,3,
3,3,3,3,3,3,3,3,3,3,3,3,3,3,3,3,3,3,3,3,4),(7.94234078979936,7.99069159969502,
8.0940913187467,8.19733761942809,8.30046263334334,8.4035222658568,8.50655054683657,
8.60958146299715,8.71271926917291,8.8159133887099,8.91929033584984,8.98952804965688,
9.09292506063529,9.19616867374971,9.29929104430254,9.40234806209879,9.50537376095564,
9.60840213156772,9.71153746675316,9.81472915320384,9.9181037560014,9.98836449961875,
10.0917566178357,10.1949952392422,10.2981124942289,10.4011643228401,10.5041847663884,
10.6072078229917,10.7103377901475,10.8135240700051,10.9168932637763,10.9872009495806,
11.0905965455969,11.1938386948507,11.2969595353445,11.4000149830984,11.5030390741534,
11.6060658013884,11.7091994494476,11.8123894216688,11.91576228528,11.9860373995425,
12.0894323593401,12.192673870897,12.2957940746466,12.3988488865806,12.5018723436841,
12.6048984397812,12.7080314654776,12.8112208192822,12.9145930777863,12.9848738495044,
13.0869196151459,13.1887917827773,13.2905669746092,13.3922809415229,13.4939693493735,
13.5957283273467,13.697522002645,13.7994743418109,13.8757070301447),
 .UNSPECIFIED.);
#1978=B_SPLINE_CURVE_WITH_KNOTS('',3,(#193532,#193533,#193534,#193535,#193536,
#193537,#193538,#193539,#193540,#193541,#193542,#193543,#193544,#193545,
#193546,#193547,#193548,#193549,#193550,#193551,#193552,#193553,#193554,
#193555,#193556,#193557,#193558,#193559,#193560,#193561,#193562,#193563,
#193564,#193565,#193566,#193567,#193568,#193569,#193570,#193571,#193572,
#193573,#193574,#193575,#193576,#193577,#193578,#193579,#193580,#193581,
#193582,#193583,#193584,#193585,#193586,#193587,#193588,#193589,#193590,
#193591,#193592,#193593,#193594,#193595,#193596,#193597,#193598,#193599,
#193600,#193601,#193602,#193603,#193604,#193605,#193606,#193607,#193608,
#193609,#193610,#193611,#193612,#193613,#193614,#193615,#193616,#193617,
#193618,#193619,#193620,#193621,#193622,#193623,#193624,#193625,#193626,
#193627,#193628,#193629,#193630,#193631,#193632,#193633,#193634,#193635,
#193636,#193637,#193638,#193639,#193640,#193641,#193642,#193643,#193644,
#193645,#193646,#193647,#193648,#193649,#193650,#193651,#193652,#193653,
#193654,#193655,#193656,#193657,#193658,#193659,#193660,#193661,#193662,
#193663,#193664,#193665,#193666,#193667,#193668,#193669,#193670,#193671,
#193672,#193673,#193674,#193675,#193676,#193677,#193678,#193679,#193680,
#193681,#193682,#193683,#193684,#193685,#193686,#193687,#193688,#193689,
#193690,#193691,#193692,#193693,#193694,#193695,#193696,#193697,#193698,
#193699,#193700,#193701,#193702,#193703,#193704,#193705,#193706,#193707,
#193708,#193709,#193710,#193711,#193712,#193713,#193714,#193715,#193716,
#193717,#193718,#193719,#193720,#193721,#193722,#193723,#193724,#193725,
#193726,#193727,#193728,#193729,#193730,#193731,#193732,#193733,#193734,
#193735,#193736,#193737,#193738,#193739,#193740,#193741,#193742,#193743,
#193744,#193745,#193746,#193747,#193748,#193749,#193750,#193751,#193752,
#193753,#193754,#193755,#193756,#193757),.UNSPECIFIED.,.F.,.F.,(4,2,2,2,
2,2,2,2,2,2,2,2,2,2,2,2,2,2,2,2,2,2,2,2,2,2,2,2,2,2,2,2,2,2,2,2,2,2,2,2,
2,2,2,2,2,2,2,2,2,2,2,2,2,2,2,2,2,2,2,2,2,2,2,2,2,2,2,2,2,2,2,2,2,2,2,2,
2,2,2,2,2,2,2,2,2,2,2,2,2,2,2,2,2,2,2,2,2,2,2,2,2,2,2,2,2,2,2,2,2,2,2,2,
4),(0.0747573278913931,0.0845184568723634,0.106384488924799,0.122977073836737,
0.133286041480215,0.136520206462886,0.138580647778778,0.14050665550755,
0.14302472648801,0.147271549528457,0.192337588514278,0.220917592465344,
0.234450995086863,0.241869005899496,0.243841401544,0.244851122749664,0.245918161725359,
0.247244777703299,0.249294109348943,0.258883112422578,0.318505453636211,
0.335297069016963,0.345718755640732,0.348984785040333,0.35106507308597,
0.35300944577025,0.355551442051943,0.359839148817527,0.39423292416601,0.44343534651272,
0.453287175653806,0.455474762914013,0.456715739764428,0.457792004326271,
0.45917066473234,0.462028553635301,0.484805755916712,0.527329183667635,
0.545904430961908,0.557102184503488,0.560449702389093,0.562545367444631,
0.564479109101443,0.566971932534784,0.571099455013165,0.598278134504166,
0.64034775302055,0.656908101261101,0.665449578366819,0.667534910396288,
0.668750040287345,0.669826490989463,0.671211225752069,0.673503625263376,
0.687287701042015,0.69862097868883,0.737949750063071,0.764492311579503,
0.770660371029709,0.773322010667461,0.775273834943801,0.777074351130886,
0.77998935283224,0.787184856519674,0.833862854130476,0.856213797873246,
0.870037658861674,0.875062782863863,0.878645304219324,0.880154598875101,
0.881246034459896,0.882271318788963,0.884011292777907,0.888723650256947,
0.929075020144451,0.977358997253004,0.982966736376446,0.985529993712516,
0.987467669503632,0.989297536027248,0.99185014953113,0.998557336409075,
1.05366060343261,1.07817670201039,1.0891211898708,1.0913732874147,1.09262570405227,
1.09369780479726,1.09505199430249,1.09779133537881,1.11614974346584,1.16514968870468,
1.18898303046794,1.19480675283253,1.19740895939576,1.19935225050625,1.20117010854636,
1.20367846980671,1.21011173969497,1.26784055833987,1.29070305368072,1.30119586102782,
1.30341928450233,1.30466495407273,1.30573723565602,1.30709916485218,1.30978755097911,
1.32763514925058,1.33373204695253,1.37574263655658,1.40292854304668,1.40705404623529,
1.40817977152992),.UNSPECIFIED.);
#1979=B_SPLINE_CURVE_WITH_KNOTS('',3,(#193762,#193763,#193764,#193765,#193766,
#193767,#193768,#193769,#193770,#193771,#193772,#193773,#193774,#193775,
#193776,#193777,#193778,#193779,#193780,#193781,#193782,#193783,#193784,
#193785,#193786,#193787,#193788,#193789,#193790,#193791,#193792,#193793,
#193794,#193795,#193796,#193797,#193798,#193799,#193800,#193801,#193802,
#193803,#193804,#193805,#193806,#193807,#193808,#193809,#193810,#193811,
#193812,#193813,#193814,#193815,#193816,#193817,#193818,#193819,#193820,
#193821,#193822,#193823,#193824,#193825,#193826,#193827,#193828,#193829,
#193830,#193831,#193832,#193833,#193834,#193835,#193836,#193837,#193838,
#193839,#193840,#193841,#193842,#193843,#193844,#193845,#193846,#193847,
#193848,#193849,#193850,#193851,#193852,#193853,#193854,#193855,#193856,
#193857,#193858,#193859,#193860,#193861,#193862,#193863,#193864,#193865,
#193866,#193867,#193868,#193869,#193870,#193871,#193872,#193873,#193874,
#193875,#193876,#193877,#193878,#193879,#193880,#193881,#193882,#193883,
#193884,#193885,#193886,#193887,#193888,#193889,#193890,#193891,#193892,
#193893,#193894,#193895,#193896,#193897,#193898,#193899,#193900,#193901,
#193902,#193903,#193904,#193905,#193906,#193907,#193908,#193909,#193910,
#193911,#193912,#193913,#193914,#193915,#193916,#193917,#193918,#193919,
#193920,#193921,#193922,#193923,#193924,#193925,#193926,#193927,#193928,
#193929,#193930,#193931,#193932,#193933,#193934,#193935,#193936,#193937,
#193938,#193939,#193940,#193941,#193942,#193943,#193944,#193945,#193946,
#193947,#193948,#193949,#193950,#193951,#193952,#193953,#193954,#193955,
#193956,#193957,#193958,#193959,#193960,#193961,#193962,#193963,#193964,
#193965,#193966,#193967,#193968,#193969,#193970,#193971,#193972,#193973,
#193974,#193975,#193976,#193977,#193978,#193979,#193980,#193981,#193982,
#193983,#193984,#193985,#193986,#193987,#193988,#193989,#193990,#193991,
#193992,#193993,#193994,#193995,#193996,#193997,#193998,#193999),
 .UNSPECIFIED.,.F.,.F.,(4,2,2,2,2,2,2,2,2,2,2,2,2,2,2,2,2,2,2,2,2,2,2,2,
2,2,2,2,2,2,2,2,2,2,2,2,2,2,2,2,2,2,2,2,2,2,2,2,2,2,2,2,2,2,2,2,2,2,2,2,
2,2,2,2,2,2,2,2,2,2,2,2,2,2,2,2,2,2,2,2,2,2,2,2,2,2,2,2,2,2,2,2,2,2,2,2,
2,2,2,2,2,2,2,2,2,2,2,2,2,2,2,2,2,2,2,2,2,2,4),(1.26014529339144,1.26297464047121,
1.26555236723457,1.26749233441503,1.2693180147951,1.27185459848015,1.27845859063422,
1.33470346965188,1.35365868098231,1.36866297404335,1.37101332824703,1.37241600397414,
1.37349575110534,1.37470248195186,1.37674797261363,1.38479359426047,1.39993588627135,
1.43964131592529,1.47090170089244,1.47512868593201,1.47765059794279,1.47958877742304,
1.48167137717811,1.48495983582815,1.49561488389859,1.5129447246226,1.55323577024489,
1.58023210347049,1.58313478647756,1.5845214770423,1.5855964955573,1.58682651772072,
1.58897712332772,1.5983743876709,1.64761815055298,1.6828408894392,1.6871385356592,
1.68968094602136,1.69162238173212,1.69369632858282,1.696945632746,1.70725531277231,
1.72381415334077,1.7567055088474,1.77026169396841,1.77757609119675,1.78191649753897,
1.79309983972583,1.79525482756751,1.7966139394648,1.79768639494436,1.79893501072878,
1.80117058855457,1.81184953177432,1.83537668589542,1.89203012686887,1.89858598361363,
1.90111475535078,1.90293828754355,1.90487918603592,1.90746364353385,1.91318707955642,
1.93626122682681,1.96949461915746,1.99168668419642,2.00493620480639,2.00720423123931,
2.00858258859569,2.00965907517461,2.01087962134308,2.01298790445359,2.02181641686492,
2.03922372257643,2.0891080218214,2.10792309328548,2.11166728769388,2.11407096925926,
2.11598841192212,2.11815423043834,2.12181980478344,2.13646359084584,2.16403801057788,
2.19307511410123,2.21638807851245,2.21924821682677,2.22062641212825,2.22170037777364,
2.22293543219521,2.22510965790808,2.23484893066339,2.28378537384592,2.31891048836793,
2.32320602849357,2.32574754257893,2.32768849518688,2.3297621211283,2.33301132997924,
2.34332414180407,2.35989128493126,2.39134215898152,2.4284352304507,2.43127319634106,
2.43264700949187,2.4337205416077,2.43493360054744,2.43703639558514,2.43963351673771,
2.44504314187052,2.46045902525304,2.50150255754408,2.53107943269,2.53526960368001,
2.53778045354652,2.53971652310281,2.54180316017597,2.5451114364364,2.55595042400506,
2.57369920292217,2.59392175456229),.UNSPECIFIED.);
#1980=B_SPLINE_CURVE_WITH_KNOTS('',3,(#194001,#194002,#194003,#194004,#194005,
#194006,#194007,#194008,#194009,#194010,#194011,#194012,#194013,#194014,
#194015,#194016,#194017,#194018,#194019,#194020,#194021,#194022,#194023,
#194024,#194025,#194026,#194027,#194028,#194029,#194030,#194031,#194032,
#194033,#194034,#194035,#194036,#194037,#194038,#194039,#194040,#194041,
#194042,#194043,#194044,#194045,#194046,#194047,#194048,#194049,#194050,
#194051,#194052,#194053,#194054,#194055,#194056,#194057,#194058,#194059,
#194060,#194061,#194062,#194063,#194064,#194065,#194066,#194067,#194068,
#194069,#194070,#194071,#194072,#194073,#194074,#194075,#194076,#194077,
#194078,#194079,#194080,#194081,#194082,#194083,#194084,#194085,#194086,
#194087,#194088,#194089,#194090,#194091,#194092,#194093,#194094,#194095,
#194096,#194097,#194098,#194099,#194100,#194101,#194102,#194103,#194104,
#194105,#194106,#194107,#194108,#194109,#194110,#194111,#194112,#194113,
#194114,#194115,#194116,#194117,#194118,#194119,#194120,#194121,#194122,
#194123,#194124,#194125,#194126,#194127,#194128,#194129,#194130,#194131,
#194132,#194133,#194134,#194135,#194136,#194137,#194138,#194139,#194140,
#194141,#194142,#194143,#194144,#194145,#194146,#194147,#194148,#194149,
#194150,#194151,#194152,#194153,#194154,#194155,#194156,#194157,#194158,
#194159,#194160,#194161,#194162,#194163,#194164,#194165,#194166,#194167,
#194168,#194169,#194170,#194171,#194172,#194173,#194174,#194175,#194176,
#194177,#194178,#194179,#194180,#194181,#194182,#194183,#194184,#194185,
#194186,#194187,#194188,#194189,#194190,#194191,#194192,#194193,#194194,
#194195,#194196,#194197,#194198,#194199,#194200,#194201,#194202,#194203,
#194204,#194205,#194206,#194207,#194208,#194209,#194210),.UNSPECIFIED.,
 .F.,.F.,(4,2,2,2,2,2,2,2,2,2,2,2,2,2,2,2,2,2,2,2,2,2,2,2,2,2,2,2,2,2,2,
2,2,2,2,2,2,2,2,2,2,2,2,2,2,2,2,2,2,2,2,2,2,2,2,2,2,2,2,2,2,2,2,2,2,2,2,
2,2,2,2,2,2,2,2,2,2,2,2,2,2,2,2,2,2,2,2,2,2,2,2,2,2,2,2,2,2,2,2,2,2,2,2,
2,4),(1.40817977152992,1.40954560710164,1.41147833499254,1.41357286149577,
1.41691845607658,1.42810816125348,1.446667035395,1.49069771000593,1.49656846812303,
1.51244824665426,1.51506158779642,1.51640744933461,1.51747862250971,1.51873640666159,
1.52101504384949,1.53242878693592,1.55875566711102,1.61123417855208,1.61816334709237,
1.6210357693046,1.62282983413917,1.62479052494421,1.62749309573695,1.63388987049344,
1.68178411506865,1.72137471504812,1.72610769463321,1.72785089316597,1.72887687619305,
1.72996904263184,1.73147806597397,1.73505279712531,1.77424410856813,1.8229813441372,
1.83011233352274,1.83301823777969,1.83481838319174,1.83677396295087,1.83944821285175,
1.84567967409462,1.87271723788112,1.91343293580722,1.93614245550613,1.93899622171256,
1.94037303639201,1.94144672013567,1.94268234535814,1.94485971688534,1.95464848026898,
2.00353420224454,2.03864073142966,2.04293542590678,2.04547648713978,2.04741712101568,
2.04949043254769,2.0527392028345,2.06305107008396,2.07961708842125,2.11250735084954,
2.12706716039433,2.13238510253001,2.14842386248627,2.1510451319288,2.15239273654899,
2.15346400760861,2.15472038582165,2.15699286488075,2.1683014188057,2.19421481590956,
2.24727744647852,2.25416198487916,2.25702685337156,2.25881938848315,2.26078096900714,
2.2634894600511,2.26992243433805,2.29862656765248,2.34984819605326,2.3608812887332,
2.36302655399557,2.36438247365213,2.36545436528211,2.36670456963672,2.36894860964171,
2.37977478053233,2.40384855905286,2.45963438345724,2.4662750556321,2.4688167898324,
2.47064334573534,2.47251935282139,2.47500322956724,2.47774090665828,2.48229151414849,
2.49161915572466,2.54225933502191,2.57203620462721,2.57495057631857,2.57633918951182,
2.57741401276103,2.57864192620402,2.58078442257017,2.59007760424531,2.60891629515257,
2.66742166574813),.UNSPECIFIED.);
#1981=B_SPLINE_CURVE_WITH_KNOTS('',3,(#194211,#194212,#194213,#194214),
 .UNSPECIFIED.,.F.,.F.,(4,4),(-16.7565928758252,-16.4074096477818),
 .UNSPECIFIED.);
#1982=B_SPLINE_CURVE_WITH_KNOTS('',3,(#194220,#194221,#194222,#194223,#194224,
#194225,#194226,#194227,#194228,#194229,#194230,#194231,#194232,#194233,
#194234,#194235),.UNSPECIFIED.,.F.,.F.,(4,2,2,2,2,2,2,4),(2.5939427763898,
2.64911100496539,2.65727579111078,2.66034775251964,2.66217948411756,2.66402387340263,
2.66631624952862,2.66838106686199),.UNSPECIFIED.);
#1983=B_SPLINE_CURVE_WITH_KNOTS('',3,(#194236,#194237,#194238,#194239,#194240,
#194241,#194242,#194243,#194244,#194245,#194246,#194247,#194248,#194249,
#194250,#194251,#194252,#194253,#194254,#194255,#194256,#194257,#194258,
#194259,#194260,#194261,#194262,#194263,#194264,#194265,#194266,#194267,
#194268,#194269,#194270,#194271,#194272,#194273,#194274,#194275,#194276,
#194277,#194278,#194279,#194280,#194281,#194282,#194283,#194284,#194285,
#194286,#194287,#194288,#194289,#194290,#194291,#194292,#194293,#194294,
#194295,#194296,#194297,#194298,#194299,#194300,#194301,#194302,#194303,
#194304,#194305,#194306,#194307,#194308,#194309,#194310,#194311,#194312,
#194313,#194314,#194315,#194316,#194317,#194318,#194319,#194320,#194321,
#194322,#194323,#194324,#194325,#194326,#194327,#194328,#194329,#194330,
#194331,#194332,#194333,#194334,#194335,#194336,#194337,#194338,#194339,
#194340,#194341,#194342,#194343,#194344,#194345,#194346,#194347,#194348,
#194349,#194350,#194351,#194352,#194353,#194354,#194355,#194356,#194357,
#194358,#194359,#194360,#194361,#194362,#194363,#194364,#194365,#194366,
#194367,#194368,#194369,#194370,#194371,#194372,#194373,#194374,#194375,
#194376,#194377,#194378,#194379,#194380,#194381,#194382,#194383,#194384,
#194385,#194386,#194387,#194388,#194389,#194390,#194391,#194392,#194393,
#194394,#194395,#194396,#194397,#194398,#194399,#194400,#194401,#194402,
#194403,#194404,#194405,#194406,#194407,#194408,#194409,#194410,#194411,
#194412,#194413,#194414,#194415,#194416,#194417,#194418,#194419,#194420,
#194421,#194422,#194423,#194424,#194425,#194426,#194427,#194428,#194429,
#194430,#194431,#194432,#194433,#194434,#194435,#194436,#194437,#194438,
#194439,#194440,#194441,#194442,#194443,#194444,#194445,#194446,#194447,
#194448,#194449,#194450,#194451,#194452,#194453,#194454,#194455,#194456,
#194457,#194458,#194459,#194460,#194461,#194462,#194463,#194464,#194465,
#194466,#194467,#194468,#194469,#194470,#194471,#194472,#194473,#194474,
#194475,#194476,#194477,#194478,#194479,#194480,#194481,#194482,#194483,
#194484,#194485,#194486,#194487),.UNSPECIFIED.,.F.,.F.,(4,2,2,2,2,2,2,2,
2,2,2,2,2,2,2,2,2,2,2,2,2,2,2,2,2,2,2,2,2,2,2,2,2,2,2,2,2,2,2,2,2,2,2,2,
2,2,2,2,2,2,2,2,2,2,2,2,2,2,2,2,2,2,2,2,2,2,2,2,2,2,2,2,2,2,2,2,2,2,2,2,
2,2,2,2,2,2,2,2,2,2,2,2,2,2,2,2,2,2,2,2,2,2,2,2,2,2,2,2,2,2,2,2,2,2,2,2,
2,2,2,2,2,2,2,2,2,4),(0.000823825197108989,0.00400945008563605,0.0104637827734715,
0.0609493693956797,0.0860173114433529,0.0971066951178503,0.0993664141855828,
0.100619998727938,0.101691504613244,0.103042734738811,0.105680874999083,
0.122156709361488,0.172105754414404,0.190189888152416,0.201175646680102,
0.203636604208991,0.205921753369301,0.205936334788996,0.205951510161678,
0.205967318969076,0.205983804396929,0.206001013822833,0.206018999431138,
0.206037818701473,0.2060575352396,0.206078219659453,0.206099950534169,0.206122815608128,
0.206146913284508,0.20617235431584,0.206199263901127,0.206227784226489,
0.206258077562141,0.206290330162048,0.206324757003612,0.20636160834815,
0.206401176938608,0.206443806358067,0.208321239629732,0.210755229228764,
0.215433670312416,0.250555505648697,0.29950005778079,0.309248472817553,
0.311423081347828,0.312658085391576,0.313731840173607,0.315109537400538,
0.317967874933001,0.353828595109926,0.386598389472844,0.409207048056845,
0.414867595734132,0.417440163230724,0.419378833009472,0.421205190150472,
0.423745755827132,0.430378023195683,0.486305361914658,0.510318387916333,
0.521127860127566,0.523371066138102,0.524621160516376,0.525693173261203,
0.52704951776782,0.529711009742722,0.546792814120082,0.555102456937598,
0.565638158030108,0.59847270441242,0.615002218808887,0.625298987067793,
0.628546307193363,0.630619495712637,0.632560579126951,0.635103045533725,
0.639401978915324,0.674781700322757,0.723973283194637,0.733291858361445,
0.735436533521945,0.736665093209176,0.737740095302287,0.739128418474605,
0.742040359487207,0.773906432611635,0.777744915834216,0.810547269846879,
0.833200978877344,0.838868146716202,0.841442243238062,0.843381464312925,
0.845207899677868,0.847747866938959,0.854374387878647,0.910387711871419,
0.934356207047114,0.94515451905543,0.947397371356511,0.948647544277521,
0.949719794415094,0.95107665750154,0.953224333347304,0.964289920602169,
1.01543693676616,1.04416538621516,1.05060272632574,1.05331248660352,1.05527478220288,
1.05706783416788,1.05993321980338,1.06681737249372,1.1199705330045,1.14587183848024,
1.15717826179401,1.15945119770653,1.16070793268664,1.1617795878345,1.16312776624361,
1.16575038791887,1.18180028426588,1.18591196532136,1.20160576350127,1.23449786883911,
1.25728867247218,1.26014529339144),.UNSPECIFIED.);
#1984=B_SPLINE_CURVE_WITH_KNOTS('',3,(#194489,#194490,#194491,#194492,#194493,
#194494,#194495,#194496,#194497,#194498),.UNSPECIFIED.,.F.,.F.,(4,1,1,1,
1,1,1,4),(-22.6905949549614,-21.9744018991612,-20.9755654491994,-19.9767289992375,
-18.9778925492756,-17.9790560993137,-16.9802196493519,-16.7565928758252),
 .UNSPECIFIED.);
#1985=B_SPLINE_CURVE_WITH_KNOTS('',3,(#194499,#194500,#194501,#194502,#194503,
#194504,#194505,#194506,#194507,#194508,#194509,#194510,#194511,#194512,
#194513,#194514,#194515,#194516,#194517,#194518),.UNSPECIFIED.,.F.,.F.,
(4,2,2,2,2,2,2,2,2,4),(0.000629330687125576,0.0481769840684086,0.0539096608571859,
0.0578765520360831,0.0594500272904705,0.0605539083195781,0.0615639069530703,
0.0632252827349632,0.0674368411984206,0.0747600637111309),.UNSPECIFIED.);
#1986=B_SPLINE_CURVE_WITH_KNOTS('',3,(#194523,#194524,#194525,#194526,#194527,
#194528,#194529,#194530,#194531,#194532,#194533,#194534,#194535,#194536,
#194537,#194538,#194539,#194540,#194541,#194542,#194543,#194544,#194545,
#194546,#194547,#194548,#194549,#194550,#194551,#194552,#194553,#194554,
#194555,#194556,#194557,#194558,#194559,#194560,#194561,#194562,#194563,
#194564,#194565,#194566,#194567,#194568,#194569,#194570,#194571,#194572,
#194573,#194574,#194575,#194576,#194577,#194578,#194579,#194580,#194581,
#194582,#194583,#194584,#194585,#194586,#194587,#194588,#194589,#194590,
#194591,#194592,#194593,#194594,#194595,#194596,#194597,#194598,#194599,
#194600,#194601,#194602,#194603,#194604,#194605,#194606,#194607,#194608,
#194609,#194610,#194611,#194612,#194613,#194614,#194615,#194616,#194617,
#194618,#194619,#194620,#194621,#194622,#194623,#194624,#194625,#194626,
#194627,#194628,#194629,#194630,#194631,#194632,#194633,#194634,#194635,
#194636,#194637,#194638,#194639,#194640,#194641,#194642,#194643,#194644,
#194645,#194646,#194647,#194648,#194649,#194650,#194651,#194652,#194653,
#194654,#194655,#194656,#194657,#194658,#194659,#194660,#194661,#194662,
#194663,#194664,#194665,#194666,#194667,#194668,#194669,#194670,#194671,
#194672,#194673,#194674,#194675,#194676,#194677,#194678,#194679,#194680,
#194681,#194682,#194683,#194684,#194685,#194686,#194687,#194688,#194689,
#194690,#194691,#194692,#194693,#194694,#194695,#194696,#194697,#194698,
#194699,#194700,#194701,#194702,#194703,#194704,#194705,#194706,#194707,
#194708,#194709,#194710,#194711,#194712,#194713,#194714,#194715,#194716,
#194717,#194718,#194719,#194720,#194721,#194722,#194723,#194724,#194725,
#194726,#194727,#194728,#194729,#194730,#194731,#194732,#194733,#194734,
#194735,#194736,#194737,#194738,#194739,#194740,#194741,#194742,#194743,
#194744,#194745,#194746,#194747,#194748,#194749,#194750,#194751,#194752,
#194753,#194754,#194755,#194756,#194757,#194758),.UNSPECIFIED.,.F.,.F.,
(4,2,2,2,2,2,2,2,2,2,2,2,2,2,2,2,2,2,2,2,2,2,2,2,2,2,2,2,2,2,2,2,2,2,2,
2,2,2,2,2,2,2,2,2,2,2,2,2,2,2,2,2,2,2,2,2,2,2,2,2,2,2,2,2,2,2,2,2,2,2,2,
2,2,2,2,2,2,2,2,2,2,2,2,2,2,2,2,2,2,2,2,2,2,2,2,2,2,2,2,2,2,2,2,2,2,2,2,
2,2,2,2,2,2,2,2,2,2,4),(1.26007673425044,1.27822034854057,1.28180703240457,
1.28331831114579,1.28441105158424,1.28543667815149,1.28717748420687,1.2918935596457,
1.33231247703275,1.33420232974193,1.37803753563163,1.3852611505755,1.38818306366884,
1.38998649676569,1.39194043723396,1.39460310102582,1.40076525819235,1.42723729776746,
1.46616241659447,1.4743072172829,1.49158433063981,1.49425345966724,1.49561158988127,
1.49668392576704,1.49793315382893,1.50017169869674,1.51090010700594,1.53460879252624,
1.56198738678538,1.593925215884,1.5981657104196,1.6006914456784,1.60263009810805,
1.60471079073515,1.60799112759627,1.61857517009446,1.63574574563707,1.68149473027648,
1.68826406879547,1.70371146986738,1.70607984863648,1.70748773331768,1.70856814014955,
1.70977190125538,1.71180428465049,1.71969762708589,1.7344197029257,1.76346395810338,
1.80585899123358,1.81015301786832,1.81269432862232,1.81463552477766,1.81670979776849,
1.81996082859284,1.83028624203308,1.84688011726286,1.87979983748303,1.89584072437233,
1.89963267018512,1.91567456110945,1.91829658453125,1.91964461961337,1.92071624670885,
1.92197305414485,1.92424637760147,1.93556052225193,1.9614898725518,2.01455864423808,
2.02144645474548,2.02431241178301,2.02610554847049,2.02806772322619,2.03077691704051,
2.0372110005296,2.06591631435643,2.11717680274213,2.12820320396987,2.13034851468667,
2.13170466851684,2.13277688686089,2.13402763747206,2.136273049107,2.14711334411419,
2.17123427606813,2.22697591490186,2.2336268322301,2.23617066276573,2.23799815152965,
2.23993690430015,2.24250767285752,2.24815647689199,2.27067646789451,2.30342178835782,
2.33947784842715,2.3423392854123,2.34371780249772,2.34479187658871,2.34602689572929,
2.34820067608323,2.35793165099402,2.40687999208181,2.44200406854333,2.44668309419899,
2.4491176244479,2.45098803547697,2.45307413470562,2.45525721240222,2.45847309220987,
2.49361008414377,2.54942123335573,2.55370206928047,2.5553750573199,2.55638754917169,
2.55749003764377,2.55905457790401,2.56296312587904,2.58213095395406,2.5939427763898),
 .UNSPECIFIED.);
#1987=B_SPLINE_CURVE_WITH_KNOTS('',3,(#194759,#194760,#194761,#194762,#194763,
#194764,#194765,#194766,#194767,#194768,#194769,#194770,#194771,#194772,
#194773,#194774,#194775,#194776,#194777,#194778,#194779,#194780,#194781,
#194782,#194783,#194784,#194785,#194786,#194787,#194788,#194789,#194790,
#194791,#194792,#194793,#194794,#194795,#194796,#194797,#194798,#194799,
#194800,#194801,#194802,#194803,#194804,#194805,#194806,#194807,#194808,
#194809,#194810,#194811,#194812,#194813,#194814,#194815,#194816,#194817,
#194818,#194819,#194820,#194821,#194822,#194823,#194824,#194825,#194826,
#194827,#194828,#194829,#194830,#194831,#194832,#194833,#194834,#194835,
#194836,#194837,#194838,#194839,#194840,#194841,#194842,#194843,#194844,
#194845,#194846,#194847,#194848,#194849,#194850,#194851,#194852,#194853,
#194854,#194855,#194856,#194857,#194858,#194859,#194860,#194861,#194862,
#194863,#194864,#194865,#194866,#194867,#194868,#194869,#194870,#194871,
#194872,#194873,#194874,#194875,#194876,#194877,#194878,#194879,#194880,
#194881,#194882,#194883,#194884,#194885,#194886,#194887,#194888,#194889,
#194890,#194891,#194892,#194893,#194894,#194895,#194896,#194897,#194898,
#194899,#194900,#194901,#194902,#194903,#194904,#194905,#194906,#194907,
#194908,#194909,#194910,#194911,#194912,#194913,#194914,#194915,#194916,
#194917,#194918,#194919,#194920,#194921,#194922,#194923,#194924,#194925,
#194926,#194927,#194928,#194929,#194930,#194931,#194932,#194933,#194934,
#194935,#194936,#194937,#194938,#194939,#194940,#194941,#194942,#194943,
#194944,#194945,#194946,#194947,#194948,#194949,#194950,#194951,#194952,
#194953,#194954,#194955,#194956,#194957,#194958,#194959,#194960,#194961,
#194962,#194963,#194964,#194965,#194966,#194967,#194968,#194969,#194970,
#194971,#194972,#194973,#194974,#194975,#194976,#194977,#194978,#194979,
#194980),.UNSPECIFIED.,.F.,.F.,(4,2,2,2,2,2,2,2,2,2,2,2,2,2,2,2,2,2,2,2,
2,2,2,2,2,2,2,2,2,2,2,2,2,2,2,2,2,2,2,2,2,2,2,2,2,2,2,2,2,2,2,2,2,2,2,2,
2,2,2,2,2,2,2,2,2,2,2,2,2,2,2,2,2,2,2,2,2,2,2,2,2,2,2,2,2,2,2,2,2,2,2,2,
2,2,2,2,2,2,2,2,2,2,2,2,2,2,2,2,2,2,4),(0.0747600637111309,0.117105823764469,
0.145108411734536,0.159869859461584,0.16347296292742,0.16566682895406,0.167580337587679,
0.169941789263497,0.173550182604974,0.190283437410746,0.199048912005449,
0.246254159454364,0.260993802292196,0.268891893502176,0.270924206361464,
0.272127675912181,0.273207653512253,0.274614744444762,0.276981280881599,
0.29239964380829,0.299150922851425,0.344056021383004,0.36175381554568,0.372570961798037,
0.375876428823309,0.377962188704936,0.379898060862263,0.382409528472346,
0.386602676660348,0.416067874415692,0.457611867419546,0.472769410626551,
0.480818684089956,0.482863929807413,0.484070292057608,0.485149560672342,
0.486551406420661,0.488899922187192,0.503878521982589,0.524489506496471,
0.557486860936813,0.580451769821037,0.58616027768988,0.588741624185283,
0.590681652017809,0.592505441437672,0.595036286062315,0.601607314702554,
0.65812356269269,0.681751986031374,0.692456895567904,0.694693709519191,
0.695942407056806,0.697014561073142,0.698372805011686,0.700525489831871,
0.711677463574072,0.762882474824384,0.791461703959685,0.797880624094858,
0.800586935681674,0.802548298428888,0.804341574969612,0.807209663694989,
0.814112460989114,0.866991338859081,0.893070554381798,0.904421271813461,
0.90669640945359,0.90795346303484,0.909024844442683,0.91037198451393,0.912990546788288,
0.928978157107934,0.929666273628093,0.973973556302938,1.0033433745717,1.0098561001038,
1.01257826128358,1.0145425861999,1.01633273495281,1.01918318927731,1.02597855199891,
1.08018858644684,1.10535322543206,1.11646879937416,1.1187303851603,1.11998453074097,
1.12105622625253,1.12240732529864,1.12504411230898,1.14147511903859,1.19206406517171,
1.20977577121625,1.22059951292097,1.22390604391618,1.2259922561474,1.2279283973344,
1.23044000045437,1.23463290643626,1.26437719762356,1.30532176334021,1.32780172822321,
1.33046518117726,1.33180403432858,1.33277202147971,1.33399564818647,1.336118192394,
1.34513699855699,1.3631223287937,1.40833130187303),.UNSPECIFIED.);
#1988=B_SPLINE_CURVE_WITH_KNOTS('',3,(#194986,#194987,#194988,#194989,#194990,
#194991),.UNSPECIFIED.,.F.,.F.,(4,2,4),(2.59391834687278,2.60763875198809,
2.66839545987335),.UNSPECIFIED.);
#1989=B_SPLINE_CURVE_WITH_KNOTS('',3,(#194992,#194993,#194994,#194995,#194996,
#194997,#194998,#194999,#195000,#195001,#195002,#195003,#195004,#195005,
#195006,#195007,#195008,#195009,#195010,#195011,#195012,#195013,#195014,
#195015,#195016,#195017,#195018,#195019,#195020,#195021,#195022,#195023,
#195024,#195025,#195026,#195027,#195028,#195029,#195030,#195031,#195032,
#195033,#195034,#195035,#195036,#195037,#195038,#195039,#195040,#195041,
#195042,#195043,#195044,#195045,#195046,#195047,#195048,#195049,#195050,
#195051,#195052,#195053,#195054,#195055,#195056,#195057,#195058,#195059,
#195060,#195061,#195062,#195063,#195064,#195065,#195066,#195067,#195068,
#195069,#195070,#195071,#195072,#195073,#195074,#195075,#195076,#195077,
#195078,#195079,#195080,#195081,#195082,#195083,#195084,#195085,#195086,
#195087,#195088,#195089,#195090,#195091,#195092,#195093,#195094,#195095,
#195096,#195097,#195098,#195099,#195100,#195101,#195102,#195103,#195104,
#195105,#195106,#195107,#195108,#195109,#195110,#195111,#195112,#195113,
#195114,#195115,#195116,#195117,#195118,#195119,#195120,#195121,#195122,
#195123,#195124,#195125,#195126,#195127,#195128,#195129,#195130,#195131,
#195132,#195133,#195134,#195135,#195136,#195137,#195138,#195139,#195140,
#195141,#195142,#195143,#195144,#195145,#195146,#195147,#195148,#195149,
#195150,#195151,#195152,#195153,#195154,#195155,#195156,#195157,#195158,
#195159,#195160,#195161,#195162,#195163,#195164,#195165,#195166,#195167,
#195168,#195169,#195170,#195171,#195172,#195173,#195174,#195175,#195176,
#195177,#195178,#195179,#195180,#195181,#195182,#195183,#195184,#195185,
#195186,#195187,#195188,#195189,#195190,#195191,#195192,#195193,#195194,
#195195,#195196,#195197,#195198,#195199,#195200,#195201,#195202,#195203,
#195204,#195205,#195206,#195207,#195208,#195209,#195210,#195211,#195212,
#195213),.UNSPECIFIED.,.F.,.F.,(4,2,2,2,2,2,2,2,2,2,2,2,2,2,2,2,2,2,2,2,
2,2,2,2,2,2,2,2,2,2,2,2,2,2,2,2,2,2,2,2,2,2,2,2,2,2,2,2,2,2,2,2,2,2,2,2,
2,2,2,2,2,2,2,2,2,2,2,2,2,2,2,2,2,2,2,2,2,2,2,2,2,2,2,2,2,2,2,2,2,2,2,2,
2,2,2,2,2,2,2,2,2,2,2,2,2,2,2,2,2,2,4),(0.0008107227228681,0.00554261242357023,
0.00881069503303161,0.0102445751035381,0.0113189839483436,0.012341800553414,
0.0133650025371135,0.014806018979062,0.0186526202746868,0.026391011620125,
0.0473065533864827,0.0988382636989564,0.111887535807851,0.115415754172655,
0.117550594294732,0.119472508732425,0.121925303839554,0.12583219147926,
0.147488757626182,0.20735969504481,0.215841010091871,0.219420204375171,
0.221354409470144,0.222628441523035,0.223822912393626,0.224866392342224,
0.226245257493794,0.229109851175418,0.264707789076383,0.297562034167569,
0.314119270433323,0.324428098518561,0.327676447986507,0.329749626993424,
0.331690233133116,0.334231398498342,0.33852661675391,0.373664432788686,
0.422637795107076,0.432353676390653,0.434526083989274,0.435760620706204,
0.436834471006619,0.438212947314881,0.441075164761016,0.476694454306604,
0.509546977118821,0.526099969467085,0.536407142453932,0.539655495914197,
0.541728803770686,0.543669619249225,0.546211186771581,0.550507371783156,
0.585691561362842,0.634807294936188,0.644362958176063,0.646524378943076,
0.647756569447583,0.648830890689694,0.650213267092093,0.652445523957233,
0.665002294744506,0.667475806801245,0.675300191938136,0.688659867077617,
0.721518942104245,0.744263466509966,0.749942701890795,0.752518902691156,
0.754458339937502,0.756283974968964,0.758821221381019,0.765431186706561,
0.821596171725762,0.845461172322981,0.856231124784658,0.858472137223952,
0.859721854892126,0.86079406678,0.862151333628002,0.864816647440531,0.881994739114714,
0.927499393522673,0.95536265623051,0.961695939243892,0.964387960957094,
0.966346978728991,0.968143657278269,0.971029336522855,0.978037101431352,
1.02938454832566,1.05655997917679,1.06818512727908,1.07047599163981,1.07173657321053,
1.07280785023142,1.07415091403497,1.07675003518382,1.09226450802658,1.09884031895341,
1.14022790278774,1.16749905800728,1.17376032302885,1.17644008028276,1.17839698127643,
1.18019645947063,1.18309710267183,1.19019423823624,1.2398344240603,1.26007673425044),
 .UNSPECIFIED.);
#1990=B_SPLINE_CURVE_WITH_KNOTS('',3,(#195215,#195216,#195217,#195218,#195219,
#195220,#195221,#195222,#195223,#195224,#195225,#195226,#195227,#195228,
#195229,#195230,#195231,#195232,#195233,#195234,#195235,#195236,#195237,
#195238,#195239,#195240,#195241,#195242,#195243,#195244,#195245,#195246,
#195247,#195248,#195249,#195250,#195251,#195252,#195253,#195254,#195255,
#195256,#195257,#195258,#195259,#195260,#195261,#195262,#195263,#195264,
#195265,#195266,#195267,#195268,#195269,#195270,#195271,#195272,#195273,
#195274,#195275,#195276,#195277,#195278,#195279,#195280,#195281,#195282,
#195283,#195284,#195285,#195286,#195287,#195288,#195289,#195290,#195291,
#195292,#195293,#195294,#195295,#195296,#195297,#195298,#195299,#195300,
#195301,#195302,#195303,#195304,#195305,#195306,#195307,#195308,#195309,
#195310,#195311,#195312,#195313,#195314,#195315,#195316,#195317,#195318,
#195319,#195320,#195321,#195322,#195323,#195324,#195325,#195326,#195327,
#195328,#195329,#195330,#195331,#195332,#195333,#195334,#195335,#195336,
#195337,#195338,#195339,#195340,#195341,#195342,#195343,#195344,#195345,
#195346,#195347,#195348,#195349,#195350,#195351,#195352,#195353,#195354,
#195355,#195356,#195357,#195358,#195359,#195360,#195361,#195362,#195363,
#195364,#195365,#195366,#195367,#195368,#195369,#195370,#195371,#195372,
#195373,#195374,#195375,#195376,#195377,#195378,#195379,#195380,#195381,
#195382,#195383,#195384,#195385,#195386,#195387,#195388,#195389,#195390,
#195391,#195392,#195393,#195394,#195395,#195396,#195397,#195398,#195399,
#195400,#195401,#195402,#195403,#195404,#195405,#195406,#195407,#195408,
#195409,#195410,#195411,#195412,#195413,#195414,#195415,#195416,#195417,
#195418,#195419,#195420,#195421,#195422,#195423,#195424,#195425,#195426,
#195427,#195428,#195429,#195430,#195431,#195432,#195433,#195434,#195435,
#195436,#195437,#195438),.UNSPECIFIED.,.F.,.F.,(4,2,2,2,2,2,2,2,2,2,2,2,
2,2,2,2,2,2,2,2,2,2,2,2,2,2,2,2,2,2,2,2,2,2,2,2,2,2,2,2,2,2,2,2,2,2,2,2,
2,2,2,2,2,2,2,2,2,2,2,2,2,2,2,2,2,2,2,2,2,2,2,2,2,2,2,2,2,2,2,2,2,2,2,2,
2,2,2,2,2,2,2,2,2,2,2,2,2,2,2,2,2,2,2,2,2,2,2,2,2,2,2,4),(1.40833130187303,
1.41333860865638,1.43114257366929,1.43482206820683,1.43720572101494,1.43912123241566,
1.44130001566784,1.44502489346626,1.46043157714509,1.51176743708484,1.53944622634268,
1.54235321148717,1.54374053731288,1.54481539303127,1.54604449533572,1.54819176899699,
1.55754757911024,1.60681363467,1.64203742354281,1.6463341375209,1.6488759594911,
1.65081692466258,1.65289034828071,1.65613878973532,1.66644537075952,1.68299888924696,
1.71588111821047,1.7293283675807,1.73691268454139,1.75191066282938,1.75426020777919,
1.75566242103971,1.75674182470983,1.75794818579049,1.75999307995436,1.76803673881456,
1.78317585486001,1.82287756918822,1.85411741708831,1.85834284408661,1.86086389521879,
1.86280145313762,1.86488342433604,1.86817097386406,1.87882380930297,1.89615077429853,
1.94435252076409,1.94864842885042,1.95112875598218,1.96407178724157,1.96632414641052,
1.96771256316774,1.96878749452924,1.97001582243435,1.97215972501833,1.98146955642855,
2.00035926908347,2.00776456608895,2.06294338563554,2.06964714341179,2.07219886232132,
2.07402821229395,2.07596544998899,2.07852829557183,2.08413575635093,2.13242239267253,
2.17281407016494,2.177527201763,2.17926736761458,2.18029273973336,2.18138531358962,
2.18289653073126,2.18648385809957,2.22413173272559,2.2745053461978,2.28156397574394,
2.28445789874098,2.2862559270563,2.28821341550438,2.29089788613927,2.29718815722413,
2.32470420092858,2.36836192529645,2.37267676935115,2.37428700871004,2.38806817866148,
2.3903620520745,2.39174794657588,2.39282523361029,2.39404096214363,2.39612794461472,
2.40468534623343,2.42129014270033,2.46980351346381,2.49084056335534,2.49471304239968,
2.49715576049242,2.49907699874299,2.50087179399015,2.50390421111817,2.51296412135939,
2.52695566757823,2.55048381538279,2.59701886873766,2.6015925093705,2.60331145398766,
2.60433267489801,2.60542800132095,2.60695482500546,2.6106345351413,2.62772793363314,
2.66748530878275),.UNSPECIFIED.);
#1991=B_SPLINE_CURVE_WITH_KNOTS('',3,(#195439,#195440,#195441,#195442,#195443,
#195444,#195445,#195446,#195447,#195448,#195449,#195450,#195451,#195452,
#195453,#195454,#195455,#195456,#195457,#195458),.UNSPECIFIED.,.F.,.F.,
(4,2,2,2,2,2,2,2,2,4),(0.00070417545084543,0.0257174469115552,0.0359847153183718,
0.0390634835596431,0.0411897982603028,0.0432709612661059,0.0452083174595604,
0.0477298916634498,0.0519579623696429,0.0751489416222558),.UNSPECIFIED.);
#1992=B_SPLINE_CURVE_WITH_KNOTS('',3,(#195463,#195464,#195465,#195466,#195467,
#195468,#195469,#195470,#195471,#195472,#195473,#195474,#195475,#195476,
#195477,#195478,#195479,#195480,#195481,#195482,#195483,#195484,#195485,
#195486,#195487,#195488,#195489,#195490,#195491,#195492,#195493,#195494,
#195495,#195496,#195497,#195498,#195499,#195500,#195501,#195502,#195503,
#195504,#195505,#195506,#195507,#195508,#195509,#195510,#195511,#195512,
#195513,#195514,#195515,#195516,#195517,#195518,#195519,#195520,#195521,
#195522,#195523,#195524,#195525,#195526,#195527,#195528,#195529,#195530,
#195531,#195532,#195533,#195534,#195535,#195536,#195537,#195538,#195539,
#195540,#195541,#195542,#195543,#195544,#195545,#195546,#195547,#195548,
#195549,#195550,#195551,#195552,#195553,#195554,#195555,#195556,#195557,
#195558,#195559,#195560,#195561,#195562,#195563,#195564,#195565,#195566,
#195567,#195568,#195569,#195570,#195571,#195572,#195573,#195574,#195575,
#195576,#195577,#195578,#195579,#195580,#195581,#195582,#195583,#195584,
#195585,#195586,#195587,#195588,#195589,#195590,#195591,#195592,#195593,
#195594,#195595,#195596,#195597,#195598,#195599,#195600,#195601,#195602,
#195603,#195604,#195605,#195606,#195607,#195608,#195609,#195610,#195611,
#195612,#195613,#195614,#195615,#195616,#195617,#195618,#195619,#195620,
#195621,#195622,#195623,#195624,#195625,#195626,#195627,#195628,#195629,
#195630,#195631,#195632,#195633,#195634,#195635,#195636,#195637,#195638,
#195639,#195640,#195641,#195642,#195643,#195644,#195645,#195646,#195647,
#195648,#195649,#195650,#195651,#195652,#195653,#195654,#195655,#195656,
#195657,#195658,#195659,#195660,#195661,#195662,#195663,#195664,#195665,
#195666,#195667,#195668,#195669,#195670,#195671,#195672,#195673,#195674,
#195675,#195676,#195677,#195678,#195679,#195680,#195681,#195682,#195683,
#195684,#195685,#195686,#195687,#195688,#195689,#195690,#195691,#195692,
#195693,#195694,#195695,#195696,#195697,#195698,#195699,#195700,#195701,
#195702,#195703,#195704,#195705,#195706,#195707,#195708,#195709,#195710,
#195711,#195712,#195713,#195714,#195715,#195716,#195717,#195718,#195719,
#195720),.UNSPECIFIED.,.F.,.F.,(4,2,2,2,2,2,2,2,2,2,2,2,2,2,2,2,2,2,2,2,
2,2,2,2,2,2,2,2,2,2,2,2,2,2,2,2,2,2,2,2,2,2,2,2,2,2,2,2,2,2,2,2,2,2,2,2,
2,2,2,2,2,2,2,2,2,2,2,2,2,2,2,2,2,2,2,2,2,2,2,2,2,2,2,2,2,2,2,2,2,2,2,2,
2,2,2,2,2,2,2,2,2,2,2,2,2,2,2,2,2,2,2,2,2,2,2,2,2,2,2,2,2,2,2,2,2,2,2,2,
4),(1.2601389384112,1.26848571120951,1.29386306512029,1.2981337923634,1.30043133727047,
1.30232441885463,1.30456517505604,1.30846435779437,1.32437313367788,1.3345954363477,
1.37388000634629,1.40246435856348,1.40537692931074,1.40676548712629,1.40784063687077,
1.40906933645133,1.41121417390558,1.42053249098821,1.46970919683015,1.50507853084996,
1.50937773010662,1.51192050377761,1.51386189718617,1.51593548897102,1.51918359014323,
1.52948400804535,1.54602279695485,1.57356972315891,1.5897128114394,1.60079553270927,
1.61502899303413,1.61734549874146,1.61873815321135,1.61981643147212,1.62102850393194,
1.6230985254543,1.63144219898204,1.64742714650239,1.68974320820639,1.71735462586705,
1.72149220266191,1.72398775480773,1.72592162430201,1.72801543909652,1.73135567996895,
1.74248821906649,1.76091190748415,1.8076851920583,1.81240084874524,1.82701499017415,
1.8293486927043,1.83074640602968,1.83182536946033,1.83303460775215,1.83509180229052,
1.84327911877606,1.85881939573537,1.90032284238502,1.90898218140034,1.92987234476664,
1.93373698633006,1.93617756852023,1.93809889334153,1.94024238244839,1.94380667224902,
1.9572455905208,2.00851502522241,2.03853791306167,2.04145317401922,2.04284224972012,
2.04391744859541,2.04514581085012,2.04728913803729,2.05658666094371,2.07543536632353,
2.11584208852909,2.12810600527748,2.14271919054542,2.14650863200771,2.14872416546594,
2.15063681173404,2.15297221032833,2.15742251698649,2.18832193837449,2.23500482746476,
2.25098959188883,2.25360846515385,2.25495588708897,2.25602755630807,2.25728502709826,
2.25956111160132,2.27092105265357,2.29702895963914,2.34984912367748,2.35675668707532,
2.35962603713395,2.36141989626524,2.36338173658721,2.36608840694338,2.37250674280563,
2.40107789247664,2.44548993980825,2.4629725876277,2.46564626818871,2.46700542908534,
2.46804717172061,2.46805121058445,2.46805518170384,2.46805908643056,2.46806269178163,
2.46806628367417,2.46806986207604,2.46807342706223,2.46807697897155,2.46930022720019,
2.47061092653101,2.47263307888466,2.47644326979725,2.48570770035342,2.52349861205201,
2.53472391591848,2.56538710396664,2.56960118010839,2.57211933555201,2.5740569329087,
2.57614117350816,2.57943703814588,2.59015860341032,2.59391834687278),
 .UNSPECIFIED.);
#1993=B_SPLINE_CURVE_WITH_KNOTS('',3,(#195721,#195722,#195723,#195724,#195725,
#195726,#195727,#195728,#195729,#195730,#195731,#195732,#195733,#195734,
#195735,#195736,#195737,#195738,#195739,#195740,#195741,#195742,#195743,
#195744,#195745,#195746,#195747,#195748,#195749,#195750,#195751,#195752,
#195753,#195754,#195755,#195756,#195757,#195758,#195759,#195760,#195761,
#195762,#195763,#195764,#195765,#195766,#195767,#195768,#195769,#195770,
#195771,#195772,#195773,#195774,#195775,#195776,#195777,#195778,#195779,
#195780,#195781,#195782,#195783,#195784,#195785,#195786,#195787,#195788,
#195789,#195790,#195791,#195792,#195793,#195794,#195795,#195796,#195797,
#195798,#195799,#195800,#195801,#195802,#195803,#195804,#195805,#195806,
#195807,#195808,#195809,#195810,#195811,#195812,#195813,#195814,#195815,
#195816,#195817,#195818,#195819,#195820,#195821,#195822,#195823,#195824,
#195825,#195826,#195827,#195828,#195829,#195830,#195831,#195832,#195833,
#195834,#195835,#195836,#195837,#195838,#195839,#195840,#195841,#195842,
#195843,#195844,#195845,#195846,#195847,#195848,#195849,#195850,#195851,
#195852,#195853,#195854,#195855,#195856,#195857,#195858,#195859,#195860,
#195861,#195862,#195863,#195864,#195865,#195866,#195867,#195868,#195869,
#195870,#195871,#195872,#195873,#195874,#195875,#195876,#195877,#195878,
#195879,#195880,#195881,#195882,#195883,#195884,#195885,#195886,#195887,
#195888,#195889,#195890,#195891,#195892,#195893,#195894,#195895,#195896,
#195897,#195898,#195899,#195900,#195901,#195902,#195903,#195904,#195905,
#195906,#195907,#195908,#195909,#195910,#195911,#195912,#195913,#195914,
#195915,#195916,#195917,#195918,#195919,#195920,#195921,#195922,#195923,
#195924,#195925,#195926,#195927,#195928,#195929,#195930,#195931,#195932,
#195933,#195934,#195935,#195936,#195937,#195938,#195939,#195940,#195941,
#195942,#195943,#195944,#195945,#195946,#195947,#195948,#195949,#195950),
 .UNSPECIFIED.,.F.,.F.,(4,2,2,2,2,2,2,2,2,2,2,2,2,2,2,2,2,2,2,2,2,2,2,2,
2,2,2,2,2,2,2,2,2,2,2,2,2,2,2,2,2,2,2,2,2,2,2,2,2,2,2,2,2,2,2,2,2,2,2,2,
2,2,2,2,2,2,2,2,2,2,2,2,2,2,2,2,2,2,2,2,2,2,2,2,2,2,2,2,2,2,2,2,2,2,2,2,
2,2,2,2,2,2,2,2,2,2,2,2,2,2,2,2,2,2,4),(0.0751489416222558,0.0833456594865257,
0.10864754221125,0.136459750324486,0.145891457113087,0.148043769077378,
0.149273773130638,0.150348135853102,0.151733127922358,0.153974632457574,
0.166714949664848,0.188867173562766,0.21569261338959,0.23708058275434,0.245243765604029,
0.251221974994586,0.253843628386387,0.255799191562491,0.257598929644745,
0.260503294718212,0.267626112344298,0.316798134455025,0.355579236560289,
0.359167498122403,0.360678743855942,0.36177120001151,0.362796352525048,
0.36453591197414,0.369246038175862,0.409869321215986,0.456725005652046,
0.463118173385777,0.46581994484496,0.467780320578642,0.469574283108175,
0.472446934110405,0.47937864805976,0.531838843734116,0.558205065453623,
0.569627770358348,0.571906827484897,0.573164645626753,0.574235830387382,
0.575581644921237,0.578194468266733,0.59405289917602,0.598851304524438,
0.614070411229687,0.646945788474424,0.663526847683016,0.67384665322596,
0.677096411766376,0.679169997864278,0.681110639415376,0.683651352568231,
0.687944689278822,0.730339610113684,0.759386513383232,0.774118595635768,
0.782014101378475,0.784046281633098,0.785249771881767,0.78632983731581,
0.787737133559872,0.790104209803694,0.805533296041103,0.812266491300551,
0.826057518178759,0.858918039330953,0.875480171901036,0.885791541513573,
0.889040422040249,0.891113875162427,0.893054692357583,0.895596068400749,
0.899891495514801,0.935011543440762,0.983923408155616,0.993719891617363,
0.995897993119582,0.997133869170045,0.99820767091787,0.999584499228307,
1.00243783889395,1.02512028941744,1.03806346126668,1.070919155012,1.08747301926967,
1.09778094744985,1.10102965193598,1.10310321100586,1.10504428073002,1.10758620873773,
1.11188306484463,1.14708111471412,1.19623407094332,1.20575511777427,1.20791429692606,
1.2091460906737,1.21022063540107,1.2116040472708,1.21383943927351,1.22645184678908,
1.23297894613478,1.23811133127399,1.27817432782865,1.30767815269563,1.31208857522361,
1.31441550912619,1.31614260230727,1.31829903753282,1.321921874469,1.33437263889487,
1.38533348213424,1.40863530833717),.UNSPECIFIED.);
#1994=B_SPLINE_CURVE_WITH_KNOTS('',3,(#195956,#195957,#195958,#195959,#195960,
#195961,#195962,#195963,#195964,#195965),.UNSPECIFIED.,.F.,.F.,(4,2,2,2,
4),(2.59328305732938,2.5941665037565,2.60558384395807,2.63192422606051,
2.66742998661749),.UNSPECIFIED.);
#1995=B_SPLINE_CURVE_WITH_KNOTS('',3,(#195966,#195967,#195968,#195969,#195970,
#195971,#195972,#195973,#195974,#195975,#195976,#195977,#195978,#195979,
#195980,#195981,#195982,#195983,#195984,#195985,#195986,#195987,#195988,
#195989,#195990,#195991,#195992,#195993,#195994,#195995,#195996,#195997,
#195998,#195999,#196000,#196001,#196002,#196003,#196004,#196005,#196006,
#196007,#196008,#196009,#196010,#196011,#196012,#196013,#196014,#196015,
#196016,#196017,#196018,#196019,#196020,#196021,#196022,#196023,#196024,
#196025,#196026,#196027,#196028,#196029,#196030,#196031,#196032,#196033,
#196034,#196035,#196036,#196037,#196038,#196039,#196040,#196041,#196042,
#196043,#196044,#196045,#196046,#196047,#196048,#196049,#196050,#196051,
#196052,#196053,#196054,#196055,#196056,#196057,#196058,#196059,#196060,
#196061,#196062,#196063,#196064,#196065,#196066,#196067,#196068,#196069,
#196070,#196071,#196072,#196073,#196074,#196075,#196076,#196077,#196078,
#196079,#196080,#196081,#196082,#196083,#196084,#196085,#196086,#196087,
#196088,#196089,#196090,#196091,#196092,#196093,#196094,#196095,#196096,
#196097,#196098,#196099,#196100,#196101,#196102,#196103,#196104,#196105,
#196106,#196107,#196108,#196109,#196110,#196111,#196112,#196113,#196114,
#196115,#196116,#196117,#196118,#196119,#196120,#196121,#196122,#196123,
#196124,#196125,#196126,#196127,#196128,#196129,#196130,#196131,#196132,
#196133,#196134,#196135,#196136,#196137,#196138,#196139,#196140,#196141,
#196142,#196143,#196144,#196145,#196146,#196147,#196148,#196149,#196150,
#196151,#196152,#196153,#196154,#196155,#196156,#196157,#196158,#196159,
#196160,#196161,#196162,#196163,#196164,#196165,#196166,#196167,#196168,
#196169,#196170,#196171,#196172,#196173,#196174,#196175,#196176,#196177,
#196178,#196179,#196180,#196181,#196182,#196183,#196184,#196185,#196186,
#196187,#196188,#196189),.UNSPECIFIED.,.F.,.F.,(4,2,2,2,2,2,2,2,2,2,2,2,
2,2,2,2,2,2,2,2,2,2,2,2,2,2,2,2,2,2,2,2,2,2,2,2,2,2,2,2,2,2,2,2,2,2,2,2,
2,2,2,2,2,2,2,2,2,2,2,2,2,2,2,2,2,2,2,2,2,2,2,2,2,2,2,2,2,2,2,2,2,2,2,2,
2,2,2,2,2,2,2,2,2,2,2,2,2,2,2,2,2,2,2,2,2,2,2,2,2,2,2,4),(0.000768639498582023,
0.0217315272484726,0.0248344558655061,0.0269706893309883,0.0287699211802129,
0.0306851237252918,0.0330691911455451,0.0367508647498313,0.0545962054436122,
0.0730123204296272,0.121983893617493,0.131697533992236,0.133869690408933,
0.13510412307762,0.136177907691802,0.137556332154594,0.140418553991821,
0.17638729847915,0.209115490703129,0.225520420771702,0.232323419581674,
0.237498350490654,0.239967785147863,0.241807161787133,0.243631769465946,
0.246165868724782,0.25275760261694,0.309057718971785,0.332826434072779,
0.343569477766903,0.345808576049655,0.347057746247984,0.348129809803604,
0.349487301641194,0.351637596511629,0.362751428367892,0.413981553905409,
0.442572966181543,0.448993238362901,0.451699723192618,0.4536610672632,0.455454227428409,
0.458321913792698,0.465222622597656,0.518120530857191,0.544184625364757,
0.555531343195069,0.557806196561707,0.559063162439451,0.560134511170677,
0.56148166368482,0.56410040741,0.580092334180435,0.585074834321935,0.629895188471682,
0.648410768165046,0.659583411777325,0.662927535039469,0.665021966225238,
0.666955169792683,0.66944813535519,0.673577712389402,0.700891800706749,
0.743167029156377,0.759423241930254,0.767859946964166,0.769937280659886,
0.771150850592922,0.772228576249864,0.773618063844585,0.77592417791237,
0.789959189497695,0.791306288115643,0.798317156209952,0.811992946079054,
0.844854116707176,0.861415741952725,0.871727039809902,0.874976027613441,
0.877049580407818,0.878990512820406,0.88153207136188,0.885827877823962,
0.920960383050237,0.969907041110738,0.97966606817553,0.98184169548107,0.983077070104677,
0.984151013877942,0.985528779446391,0.988386659169844,1.01124636969443,
1.02401225745664,1.05686816352699,1.07342098760334,1.083728603505,1.08697738816565,
1.0890510413373,1.09099222931086,1.09353435569534,1.09783164470785,1.13304652148973,
1.18225211388281,1.19171617632965,1.19387141268155,1.19510238047612,1.19617712643471,
1.19756200941938,1.19980215413631,1.21250356894832,1.23488141388171,1.2601389384112),
 .UNSPECIFIED.);
#1996=B_SPLINE_CURVE_WITH_KNOTS('',3,(#196191,#196192,#196193,#196194,#196195,
#196196,#196197,#196198,#196199,#196200,#196201,#196202,#196203,#196204,
#196205,#196206,#196207,#196208,#196209,#196210,#196211,#196212,#196213,
#196214,#196215,#196216,#196217,#196218,#196219,#196220,#196221,#196222,
#196223,#196224,#196225,#196226,#196227,#196228,#196229,#196230,#196231,
#196232,#196233,#196234,#196235,#196236,#196237,#196238,#196239,#196240,
#196241,#196242,#196243,#196244,#196245,#196246,#196247,#196248,#196249,
#196250,#196251,#196252,#196253,#196254,#196255,#196256,#196257,#196258,
#196259,#196260,#196261,#196262,#196263,#196264,#196265,#196266,#196267,
#196268,#196269,#196270,#196271,#196272,#196273,#196274,#196275,#196276,
#196277,#196278,#196279,#196280,#196281,#196282,#196283,#196284,#196285,
#196286,#196287,#196288,#196289,#196290,#196291,#196292,#196293,#196294,
#196295,#196296,#196297,#196298,#196299,#196300,#196301,#196302,#196303,
#196304,#196305,#196306,#196307,#196308,#196309,#196310,#196311,#196312,
#196313,#196314,#196315,#196316,#196317,#196318,#196319,#196320,#196321,
#196322,#196323,#196324,#196325,#196326,#196327,#196328,#196329,#196330,
#196331,#196332,#196333,#196334,#196335,#196336,#196337,#196338,#196339,
#196340,#196341,#196342,#196343,#196344,#196345,#196346,#196347,#196348,
#196349,#196350,#196351,#196352,#196353,#196354,#196355,#196356,#196357,
#196358,#196359,#196360,#196361,#196362,#196363,#196364,#196365,#196366,
#196367,#196368,#196369,#196370,#196371,#196372,#196373,#196374,#196375,
#196376,#196377,#196378,#196379,#196380,#196381,#196382,#196383,#196384,
#196385,#196386,#196387,#196388,#196389,#196390,#196391,#196392,#196393,
#196394,#196395,#196396,#196397,#196398,#196399,#196400,#196401,#196402,
#196403,#196404,#196405,#196406,#196407,#196408),.UNSPECIFIED.,.F.,.F.,
(4,2,2,2,2,2,2,2,2,2,2,2,2,2,2,2,2,2,2,2,2,2,2,2,2,2,2,2,2,2,2,2,2,2,2,
2,2,2,2,2,2,2,2,2,2,2,2,2,2,2,2,2,2,2,2,2,2,2,2,2,2,2,2,2,2,2,2,2,2,2,2,
2,2,2,2,2,2,2,2,2,2,2,2,2,2,2,2,2,2,2,2,2,2,2,2,2,2,2,2,2,2,2,2,2,2,2,2,
2,4),(1.40863530833717,1.41654327343824,1.41945645940367,1.42084511671204,
1.42192025425947,1.42314884008716,1.42529324511845,1.43460606655398,1.48376512633104,
1.51915552835373,1.52345488524099,1.52599767313947,1.52793903193626,1.53001254268434,
1.53326042496439,1.54355937485508,1.56009507147325,1.59296542620313,1.6044920513517,
1.61424439728623,1.61613908864028,1.62921366902091,1.63147290717544,1.63286347558798,
1.63393874585811,1.6351659789608,1.63730450730202,1.64653781557121,1.6651859669194,
1.70931649426577,1.73179166900342,1.73573551362933,1.73820005947526,1.74012407025685,
1.74225396332416,1.74575722135842,1.75852419286517,1.78094207404634,1.81740719247911,
1.84064309321391,1.84350353440371,1.84488182184277,1.84595583435793,1.84719091509848,
1.84936512010164,1.85910320012664,1.90804312104045,1.943169257887,1.9474649539807,
1.95000656307348,1.95194758987745,1.95402129669984,1.95727063569175,1.96758388959959,
1.98415176478964,2.01704714078391,2.05265713538824,2.05552123552805,2.05690021147769,
2.0579742567883,2.05920880723788,2.0613807232419,2.07108629227125,2.12005175519484,
2.15518541461582,2.15948107319897,2.16202262533062,2.16396358860998,2.16603720815051,
2.16928636983893,2.17959871921695,2.19616481611943,2.22905803412187,2.2646664616157,
2.26753247890526,2.26891180148466,2.2699858468023,2.27122009294505,2.2733907480846,
2.28307881002717,2.33205711820898,2.36719417910864,2.37148974556877,2.37403122479423,
2.37597212179823,2.37804566025863,2.38129467344734,2.39160637063835,2.40817124775688,
2.47080847239665,2.47216976513443,2.47834307322888,2.48028134707058,2.48146408844023,
2.48249570117241,2.48390870028928,2.48692358285226,2.49102152766931,2.50129931076411,
2.52412040595402,2.57582987066577,2.58281333893934,2.58569505666905,2.58749105932933,
2.5894507754562,2.59214636207253,2.5985001675002,2.62653592440016,2.66822463298926),
 .UNSPECIFIED.);
#1997=B_SPLINE_CURVE_WITH_KNOTS('',3,(#196409,#196410,#196411,#196412,#196413,
#196414,#196415,#196416,#196417,#196418,#196419,#196420,#196421),
 .UNSPECIFIED.,.F.,.F.,(4,3,3,3,4),(-48.1740290551459,-48.0708042001896,
-47.9674104512405,-47.94414959817,-47.8233361836797),.UNSPECIFIED.);
#1998=B_SPLINE_CURVE_WITH_KNOTS('',3,(#196426,#196427,#196428,#196429,#196430,
#196431,#196432,#196433,#196434,#196435,#196436,#196437,#196438,#196439,
#196440,#196441,#196442,#196443,#196444,#196445,#196446,#196447,#196448,
#196449,#196450,#196451,#196452,#196453,#196454,#196455,#196456,#196457,
#196458,#196459,#196460,#196461,#196462,#196463,#196464,#196465,#196466,
#196467,#196468,#196469,#196470,#196471,#196472,#196473,#196474,#196475,
#196476,#196477,#196478,#196479,#196480,#196481,#196482,#196483,#196484,
#196485,#196486,#196487,#196488,#196489,#196490,#196491,#196492,#196493,
#196494,#196495,#196496,#196497,#196498,#196499,#196500,#196501,#196502,
#196503,#196504,#196505,#196506,#196507,#196508,#196509,#196510,#196511,
#196512,#196513,#196514,#196515,#196516,#196517,#196518,#196519,#196520,
#196521,#196522,#196523,#196524,#196525,#196526,#196527,#196528,#196529,
#196530,#196531,#196532,#196533,#196534,#196535,#196536,#196537,#196538,
#196539,#196540,#196541,#196542,#196543,#196544,#196545,#196546,#196547,
#196548,#196549,#196550,#196551,#196552,#196553,#196554,#196555,#196556,
#196557,#196558,#196559,#196560,#196561,#196562,#196563,#196564,#196565,
#196566,#196567,#196568,#196569,#196570,#196571,#196572,#196573,#196574,
#196575,#196576,#196577,#196578,#196579,#196580,#196581,#196582,#196583,
#196584,#196585,#196586,#196587,#196588,#196589,#196590,#196591,#196592,
#196593,#196594,#196595,#196596,#196597,#196598,#196599,#196600,#196601,
#196602,#196603,#196604,#196605,#196606,#196607,#196608,#196609,#196610,
#196611,#196612,#196613,#196614,#196615,#196616,#196617,#196618,#196619,
#196620,#196621,#196622,#196623,#196624,#196625,#196626,#196627,#196628,
#196629,#196630,#196631,#196632,#196633,#196634,#196635,#196636,#196637,
#196638,#196639,#196640,#196641,#196642,#196643,#196644,#196645,#196646,
#196647,#196648,#196649,#196650,#196651,#196652,#196653,#196654,#196655,
#196656,#196657,#196658,#196659,#196660,#196661,#196662,#196663,#196664,
#196665,#196666,#196667,#196668,#196669,#196670,#196671,#196672,#196673,
#196674,#196675,#196676,#196677,#196678,#196679,#196680,#196681,#196682,
#196683,#196684,#196685,#196686,#196687,#196688,#196689,#196690,#196691,
#196692,#196693,#196694,#196695,#196696,#196697,#196698,#196699,#196700,
#196701,#196702,#196703,#196704,#196705,#196706,#196707),.UNSPECIFIED.,
 .F.,.F.,(4,2,2,2,2,2,2,2,2,2,2,2,2,2,2,2,2,2,2,2,2,2,2,2,2,2,2,2,2,2,2,
2,2,2,2,2,2,2,2,2,2,2,2,2,2,2,2,2,2,2,2,2,2,2,2,2,2,2,2,2,2,2,2,2,2,2,2,
2,2,2,2,2,2,2,2,2,2,2,2,2,2,2,2,2,2,2,2,2,2,2,2,2,2,2,2,2,2,2,2,2,2,2,2,
2,2,2,2,2,2,2,2,2,2,2,2,2,2,2,2,2,2,2,2,2,2,2,2,2,2,2,2,2,2,2,2,2,2,2,2,
2,4),(1.2596833809502,1.28150384854047,1.30395451750715,1.31433173993329,
1.31654814463258,1.31779243049033,1.31886515460167,1.32022974891393,1.32240315902596,
1.33389986010932,1.38263545242697,1.41583873271762,1.42010258685452,1.42263487810839,
1.42457429853268,1.4266516537708,1.42991796447472,1.4403810261871,1.45728197958185,
1.49511045407783,1.52518586637426,1.52810045783411,1.52948923455204,1.53056421121483,
1.53179232990309,1.53393525621241,1.5432314121433,1.56207795393584,1.60247842875927,
1.61474052283203,1.62934635935748,1.63313463700421,1.63534962658737,1.63726188590197,
1.63959691581375,1.64404683916555,1.67495958082077,1.72180660270239,1.73760391223777,
1.74021639403696,1.74156227823741,1.74263364756808,1.74389183792505,1.74617195567225,
1.75760856869607,1.78402410843133,1.83638767113452,1.84332611747916,1.84620019751758,
1.84799465751142,1.84995526625725,1.85265678342283,1.8590466266238,1.88738482047263,
1.93728396907904,1.94991440563756,1.9521506881435,1.95353432145482,1.95460883066996,
1.955840359522,1.95799853019891,1.9675067846179,2.0166417589585,2.05182800437473,
2.05612436550452,2.05866612786458,2.06060713338944,2.06268068336504,2.06592949658284,
2.0762387215821,2.09279787942866,2.12568542647966,2.13955087604799,2.1461149157402,
2.16166397004852,2.16426435912158,2.1656075900694,2.16667874135438,2.1679388788144,
2.17022816615922,2.18182952175351,2.20890852853831,2.26033590383901,2.26733483524746,
2.27021881904326,2.27201501848728,2.27397397952619,2.27666676255737,2.28300572936343,
2.31092287826035,2.35692108319348,2.35819339220091,2.37368534805368,2.37628329366009,
2.37762599359105,2.37869710933368,2.3799576565317,2.38224884747986,2.39388454785365,
2.42110341098997,2.44129017406253,2.47581019414818,2.48009734153408,2.48263641752228,
2.48457696573734,2.48466516121913,2.48471829642163,2.48475072620655,2.48479303665328,
2.48483143129011,2.48486632749208,2.48489808952065,2.48492703666271,2.4849534516183,
2.48497758299186,2.48499965097878,2.48501985112025,2.48503835757562,2.4850553259572,
2.48507089555338,2.48509352481743,2.48511573443406,2.48513753572401,2.48515894352915,
2.48517997050377,2.48520062880447,2.48522093010883,2.48747137199418,2.49155610432155,
2.49664786551223,2.50755454423486,2.53220185164321,2.55229775944963,2.56494070528658,
2.56972246127871,2.58559872972517,2.58821236335305,2.58955843526454,2.59062974008095,
2.59188760638825,2.59328305732938),.UNSPECIFIED.);
#1999=B_SPLINE_CURVE_WITH_KNOTS('',3,(#196709,#196710,#196711,#196712,#196713,
#196714,#196715,#196716,#196717,#196718,#196719,#196720,#196721,#196722,
#196723,#196724,#196725,#196726,#196727,#196728,#196729,#196730,#196731,
#196732,#196733,#196734,#196735,#196736,#196737,#196738,#196739,#196740,
#196741,#196742,#196743,#196744,#196745,#196746,#196747,#196748,#196749,
#196750,#196751,#196752,#196753,#196754,#196755,#196756,#196757,#196758,
#196759,#196760,#196761,#196762,#196763,#196764,#196765,#196766,#196767,
#196768,#196769,#196770,#196771,#196772,#196773,#196774,#196775,#196776,
#196777,#196778,#196779,#196780,#196781,#196782,#196783,#196784,#196785,
#196786,#196787,#196788,#196789,#196790,#196791,#196792,#196793,#196794,
#196795,#196796,#196797,#196798,#196799,#196800,#196801,#196802,#196803,
#196804,#196805,#196806,#196807,#196808,#196809,#196810,#196811,#196812,
#196813,#196814,#196815,#196816,#196817,#196818,#196819,#196820,#196821,
#196822,#196823,#196824,#196825,#196826,#196827,#196828,#196829,#196830,
#196831,#196832,#196833,#196834,#196835,#196836,#196837,#196838,#196839,
#196840,#196841,#196842,#196843,#196844,#196845,#196846,#196847,#196848,
#196849,#196850,#196851,#196852,#196853,#196854,#196855,#196856,#196857,
#196858,#196859,#196860,#196861,#196862,#196863,#196864,#196865,#196866,
#196867,#196868,#196869,#196870,#196871,#196872,#196873,#196874,#196875,
#196876,#196877,#196878,#196879,#196880,#196881,#196882,#196883,#196884,
#196885,#196886),.UNSPECIFIED.,.F.,.F.,(4,3,3,3,3,3,3,3,3,3,3,3,3,3,3,3,
3,3,3,3,3,3,3,3,3,3,3,3,3,3,3,3,3,3,3,3,3,3,3,3,3,3,3,3,3,3,3,3,3,3,3,3,
3,3,3,3,3,3,3,4),(-54.1065214908593,-53.9371682979412,-53.8337735608932,
-53.7305322787781,-53.6274123133858,-53.5243577451767,-53.4213345368189,
-53.3183086941464,-53.2151759273682,-53.1119868359583,-53.0086148425766,
-52.9383318479793,-52.8349371109314,-52.7316958288165,-52.6285758634242,
-52.5255212952153,-52.4224980868577,-52.3194722441852,-52.2163394774072,
-52.1131503859974,-52.0097783926158,-51.9394953980175,-51.8361006609696,
-51.7328593788546,-51.6297394134623,-51.5266848452534,-51.4236616368957,
-51.3206357942231,-51.2175030274451,-51.1143139360353,-51.0109419426537,
-50.9406589480556,-50.8372642110076,-50.7340229288926,-50.6309029635003,
-50.5278483952914,-50.4248251869336,-50.3217993442611,-50.218666577483,
-50.1154774860732,-50.0121054926915,-49.9418224980937,-49.8384277610457,
-49.7351864789307,-49.6320665135383,-49.5290119453294,-49.4259887369716,
-49.322962894299,-49.2198301275209,-49.1166410361111,-49.0132690427294,
-48.9429860481318,-48.8396205066934,-48.7363953136927,-48.6332762150873,
-48.530229079458,-48.4271932051592,-48.3241646395798,-48.2210652727916,
-48.1740290551459),.UNSPECIFIED.);
#2000=B_SPLINE_CURVE_WITH_KNOTS('',3,(#196887,#196888,#196889,#196890),
 .UNSPECIFIED.,.F.,.F.,(4,4),(-54.4565130710325,-54.1065275202913),
 .UNSPECIFIED.);
#2001=B_SPLINE_CURVE_WITH_KNOTS('',3,(#196896,#196897,#196898,#196899,#196900,
#196901,#196902,#196903,#196904,#196905,#196906,#196907,#196908,#196909,
#196910,#196911,#196912,#196913,#196914,#196915),.UNSPECIFIED.,.F.,.F.,
(4,2,2,2,2,2,2,2,2,4),(2.59294800260859,2.59867319176495,2.60292963635251,
2.60545927305944,2.60739767247906,2.60947492156612,2.61274314334304,2.61654582757013,
2.62380936125772,2.66743053820994),.UNSPECIFIED.);
#2002=B_SPLINE_CURVE_WITH_KNOTS('',3,(#196916,#196917,#196918,#196919,#196920,
#196921,#196922,#196923,#196924,#196925,#196926,#196927,#196928,#196929,
#196930,#196931,#196932,#196933,#196934,#196935,#196936,#196937,#196938,
#196939,#196940,#196941,#196942,#196943,#196944,#196945,#196946,#196947,
#196948,#196949,#196950,#196951,#196952,#196953,#196954,#196955,#196956,
#196957,#196958,#196959,#196960,#196961,#196962,#196963,#196964,#196965,
#196966,#196967,#196968,#196969,#196970,#196971,#196972,#196973,#196974,
#196975,#196976,#196977,#196978,#196979,#196980,#196981,#196982,#196983,
#196984,#196985,#196986,#196987,#196988,#196989,#196990,#196991,#196992,
#196993,#196994,#196995,#196996,#196997,#196998,#196999,#197000,#197001,
#197002,#197003,#197004,#197005,#197006,#197007,#197008,#197009,#197010,
#197011,#197012,#197013,#197014,#197015,#197016,#197017,#197018,#197019,
#197020,#197021,#197022,#197023,#197024,#197025,#197026,#197027,#197028,
#197029,#197030,#197031,#197032,#197033,#197034,#197035,#197036,#197037,
#197038,#197039,#197040,#197041,#197042,#197043,#197044,#197045,#197046,
#197047,#197048,#197049,#197050,#197051,#197052,#197053,#197054,#197055,
#197056,#197057,#197058,#197059,#197060,#197061,#197062,#197063,#197064,
#197065,#197066,#197067,#197068,#197069,#197070,#197071,#197072,#197073,
#197074,#197075,#197076,#197077,#197078,#197079,#197080,#197081,#197082,
#197083,#197084,#197085,#197086,#197087,#197088,#197089,#197090,#197091,
#197092,#197093,#197094,#197095,#197096,#197097,#197098,#197099,#197100,
#197101,#197102,#197103,#197104,#197105,#197106,#197107,#197108,#197109,
#197110,#197111,#197112,#197113,#197114,#197115,#197116,#197117,#197118,
#197119,#197120,#197121,#197122,#197123,#197124,#197125,#197126,#197127,
#197128,#197129),.UNSPECIFIED.,.F.,.F.,(4,2,2,2,2,2,2,2,2,2,2,2,2,2,2,2,
2,2,2,2,2,2,2,2,2,2,2,2,2,2,2,2,2,2,2,2,2,2,2,2,2,2,2,2,2,2,2,2,2,2,2,2,
2,2,2,2,2,2,2,2,2,2,2,2,2,2,2,2,2,2,2,2,2,2,2,2,2,2,2,2,2,2,2,2,2,2,2,2,
2,2,2,2,2,2,2,2,2,2,2,2,2,2,2,2,2,2,4),(0.000649992353746962,0.0375152730307587,
0.0412926058670708,0.0433020332466888,0.0446072148554326,0.0458444184253734,
0.0469177310104482,0.0482917902236038,0.0511320589090229,0.0879797077658783,
0.109399199895957,0.136182386948439,0.146436084907939,0.149706952573172,
0.151785042804177,0.153723641808267,0.156252701837223,0.160506346611089,
0.193188208656405,0.222560004176568,0.244175252655833,0.254295373048069,
0.256485288615895,0.257733423610194,0.258805426931146,0.260163907219127,
0.262836050825874,0.280219443950589,0.329262044005941,0.347305210354065,
0.354573405901029,0.360002454598206,0.362567700521536,0.364505042744284,
0.366333234975281,0.368881315843799,0.375563054186285,0.430968485007962,
0.455318835720252,0.466218414143172,0.468466852460497,0.469717985888873,
0.470789734517694,0.472144264664318,0.474886021346641,0.493329699716654,
0.537460493337828,0.565331844487407,0.571665330974489,0.574356964678557,
0.576315525547254,0.57811166408164,0.580996210279416,0.587999869069225,
0.639384390969122,0.666515463046019,0.678128414208415,0.680418169282219,
0.681678310145061,0.682749314752906,0.684092166452974,0.686691253820673,
0.702216832496513,0.708761033683465,0.722633883146357,0.755493946524701,
0.772056448871761,0.782367873029121,0.785616677260266,0.787690059230241,
0.789630794048282,0.792172039462032,0.796467194770158,0.831578309325013,
0.880465442872731,0.890288619835252,0.892468477381447,0.893704709005219,
0.894778410251878,0.89615457506459,0.899004704552178,0.935374576654408,
0.989163023546042,0.995619077791897,0.998331645788874,1.00029413998966,
1.00208611342134,1.00494703966778,1.01180631807051,1.06524492489252,1.09093517112184,
1.1021865682203,1.10445598581578,1.10571179440077,1.10678327900165,1.10813203208798,
1.11075809741942,1.12692228968746,1.1775802830176,1.20199425525246,1.20789427429974,
1.21051033843575,1.21245603672437,1.21427043328026,1.2167650424735,1.2231148889465,
1.2596833809502),.UNSPECIFIED.);
#2003=B_SPLINE_CURVE_WITH_KNOTS('',3,(#197131,#197132,#197133,#197134,#197135,
#197136,#197137,#197138,#197139,#197140),.UNSPECIFIED.,.F.,.F.,(4,1,1,1,
1,1,1,4),(-60.389703770172,-59.9301869977125,-58.9313505477506,-57.9325140977887,
-56.9336776478268,-55.934841197865,-54.9360047479031,-54.4565130710325),
 .UNSPECIFIED.);
#2004=B_SPLINE_CURVE_WITH_KNOTS('',3,(#197141,#197142,#197143,#197144,#197145,
#197146,#197147,#197148,#197149,#197150,#197151,#197152,#197153,#197154,
#197155,#197156,#197157,#197158),.UNSPECIFIED.,.F.,.F.,(4,2,2,2,2,2,2,2,
4),(0.000658788806491579,0.00332970125175962,0.00592165818523893,0.00778879641236155,
0.00964368919009544,0.01149091846978,0.0146445377313671,0.0233614971653259,
0.0750737837299188),.UNSPECIFIED.);
#2005=B_SPLINE_CURVE_WITH_KNOTS('',3,(#197163,#197164,#197165,#197166,#197167,
#197168,#197169,#197170,#197171,#197172,#197173,#197174,#197175,#197176,
#197177,#197178,#197179,#197180,#197181,#197182,#197183,#197184,#197185,
#197186,#197187,#197188,#197189,#197190,#197191,#197192,#197193,#197194,
#197195,#197196,#197197,#197198,#197199,#197200,#197201,#197202,#197203,
#197204,#197205,#197206,#197207,#197208,#197209,#197210,#197211,#197212,
#197213,#197214,#197215,#197216,#197217,#197218,#197219,#197220,#197221,
#197222,#197223,#197224,#197225,#197226,#197227,#197228,#197229,#197230,
#197231,#197232,#197233,#197234,#197235,#197236,#197237,#197238,#197239,
#197240,#197241,#197242,#197243,#197244,#197245,#197246,#197247,#197248,
#197249,#197250,#197251,#197252,#197253,#197254,#197255,#197256,#197257,
#197258,#197259,#197260,#197261,#197262,#197263,#197264,#197265,#197266,
#197267,#197268,#197269,#197270,#197271,#197272,#197273,#197274,#197275,
#197276,#197277,#197278,#197279,#197280,#197281,#197282,#197283,#197284,
#197285,#197286,#197287,#197288,#197289,#197290,#197291,#197292,#197293,
#197294,#197295,#197296,#197297,#197298,#197299,#197300,#197301,#197302,
#197303,#197304,#197305,#197306,#197307,#197308,#197309,#197310,#197311,
#197312,#197313,#197314,#197315,#197316,#197317,#197318,#197319,#197320,
#197321,#197322,#197323,#197324,#197325,#197326,#197327,#197328,#197329,
#197330,#197331,#197332,#197333,#197334,#197335,#197336,#197337,#197338,
#197339,#197340,#197341,#197342,#197343,#197344,#197345,#197346,#197347,
#197348,#197349,#197350,#197351,#197352,#197353,#197354,#197355,#197356,
#197357,#197358,#197359,#197360,#197361,#197362,#197363,#197364,#197365,
#197366,#197367,#197368,#197369,#197370,#197371,#197372,#197373,#197374,
#197375,#197376,#197377,#197378,#197379,#197380,#197381,#197382,#197383,
#197384,#197385,#197386),.UNSPECIFIED.,.F.,.F.,(4,2,2,2,2,2,2,2,2,2,2,2,
2,2,2,2,2,2,2,2,2,2,2,2,2,2,2,2,2,2,2,2,2,2,2,2,2,2,2,2,2,2,2,2,2,2,2,2,
2,2,2,2,2,2,2,2,2,2,2,2,2,2,2,2,2,2,2,2,2,2,2,2,2,2,2,2,2,2,2,2,2,2,2,2,
2,2,2,2,2,2,2,2,2,2,2,2,2,2,2,2,2,2,2,2,2,2,2,2,2,2,2,4),(1.25979359209778,
1.28580300251789,1.32656732777334,1.33163306653606,1.33409244522673,1.33601522933325,
1.33814663771316,1.34165901259573,1.35453367672641,1.37723368586608,1.41581987132213,
1.42081382980198,1.43681935977937,1.43943847251636,1.44078553098614,1.44185665510057,
1.44311318950585,1.44538682444043,1.45671902871575,1.48272757550874,1.53564227689878,
1.54253696868306,1.54540328335372,1.54719591666714,1.5491569561889,1.55186351104198,
1.55828625287392,1.58690768546855,1.63818509137097,1.64924545213547,1.65139221340895,
1.65274849671124,1.65382029206697,1.65506994527921,1.65731187995249,1.66810653038302,
1.69206554581996,1.74801204116381,1.75463697406073,1.75717605825111,1.75900177749123,
1.760940163237,1.7635130158854,1.76917688315898,1.79181683313003,1.82463095132139,
1.8289272421944,1.86034481835078,1.86325618395962,1.86464406631995,1.86571864660028,
1.86694664341057,1.86909013231011,1.87840070649366,1.92754245650627,1.96290424795715,
1.96720127802684,1.96974272745421,1.97168308605368,1.97375554954224,1.97700183529579,
1.9872960918038,2.00382460357321,2.03667919229329,2.04833442764834,2.05711079036982,
2.0726980307875,2.07529928991339,2.07664240285785,2.07771315941398,2.078972482818,
2.08125939474524,2.0928296954143,2.11979059720346,2.17134758805847,2.17833456471907,
2.18121589188431,2.18301110847835,2.18496953370372,2.18766255595841,2.19400663568412,
2.22197568769335,2.26488366547887,2.26905299832699,2.28462530638709,2.28722588622606,
2.28856883530343,2.28963956022194,2.29089896157927,2.2931863102912,2.30476507748831,
2.33176070845578,2.35233787454996,2.3867184315042,2.39100143075182,2.3935387725903,
2.39547841236837,2.39755245493155,2.40080612135813,2.41096065816617,2.4272680217722,
2.46879947995584,2.49608085887807,2.49898393281528,2.50037015595383,2.50144451003423,
2.50267343373536,2.50396687137187,2.50863278756087,2.53274153999305,2.5536372827895,
2.59294800260859),.UNSPECIFIED.);
#2006=B_SPLINE_CURVE_WITH_KNOTS('',3,(#197387,#197388,#197389,#197390,#197391,
#197392,#197393,#197394,#197395,#197396,#197397,#197398,#197399,#197400,
#197401,#197402,#197403,#197404,#197405,#197406,#197407,#197408,#197409,
#197410,#197411,#197412,#197413,#197414,#197415,#197416,#197417,#197418,
#197419,#197420,#197421,#197422,#197423,#197424,#197425,#197426,#197427,
#197428,#197429,#197430,#197431,#197432,#197433,#197434,#197435,#197436,
#197437,#197438,#197439,#197440,#197441,#197442,#197443,#197444,#197445,
#197446,#197447,#197448,#197449,#197450,#197451,#197452,#197453,#197454,
#197455,#197456,#197457,#197458,#197459,#197460,#197461,#197462,#197463,
#197464,#197465,#197466,#197467,#197468,#197469,#197470,#197471,#197472,
#197473,#197474,#197475,#197476,#197477,#197478,#197479,#197480,#197481,
#197482,#197483,#197484,#197485,#197486,#197487,#197488,#197489,#197490,
#197491,#197492,#197493,#197494,#197495,#197496,#197497,#197498,#197499,
#197500,#197501,#197502,#197503,#197504,#197505,#197506,#197507,#197508,
#197509,#197510,#197511,#197512,#197513,#197514,#197515,#197516,#197517,
#197518,#197519,#197520,#197521,#197522,#197523,#197524,#197525,#197526,
#197527,#197528,#197529,#197530,#197531,#197532,#197533,#197534,#197535,
#197536,#197537,#197538,#197539,#197540,#197541,#197542,#197543,#197544,
#197545,#197546,#197547,#197548,#197549,#197550,#197551,#197552,#197553,
#197554,#197555,#197556,#197557,#197558,#197559,#197560,#197561,#197562,
#197563,#197564,#197565,#197566,#197567,#197568,#197569,#197570,#197571,
#197572,#197573,#197574,#197575,#197576,#197577,#197578,#197579,#197580,
#197581,#197582,#197583,#197584,#197585,#197586,#197587,#197588,#197589,
#197590,#197591,#197592,#197593,#197594,#197595,#197596,#197597,#197598,
#197599,#197600,#197601,#197602,#197603,#197604,#197605,#197606,#197607,
#197608,#197609,#197610,#197611,#197612,#197613,#197614,#197615,#197616,
#197617,#197618,#197619,#197620,#197621,#197622,#197623,#197624),
 .UNSPECIFIED.,.F.,.F.,(4,2,2,2,2,2,2,2,2,2,2,2,2,2,2,2,2,2,2,2,2,2,2,2,
2,2,2,2,2,2,2,2,2,2,2,2,2,2,2,2,2,2,2,2,2,2,2,2,2,2,2,2,2,2,2,2,2,2,2,2,
2,2,2,2,2,2,2,2,2,2,2,2,2,2,2,2,2,2,2,2,2,2,2,2,2,2,2,2,2,2,2,2,2,2,2,2,
2,2,2,2,2,2,2,2,2,2,2,2,2,2,2,2,2,2,2,2,2,2,4),(0.0750737837299188,0.0897196818521214,
0.108795497230402,0.112693442247156,0.114256020592199,0.115357910077045,
0.116370459886175,0.118044759042156,0.12233532342493,0.170549693967141,
0.208879267552393,0.213931672917246,0.216874072207978,0.219503902802471,
0.221426789661721,0.223219057645675,0.226081713437894,0.232939565419232,
0.286353451360456,0.312059786394583,0.323315248293243,0.325584878079516,
0.32684072198318,0.327912186782429,0.329260851318762,0.331886556676403,
0.348042510349904,0.398689539703308,0.41655022562366,0.427439013049778,
0.430752521188773,0.432840181379354,0.434775636168728,0.43728347963043,
0.441463826026978,0.470473280170901,0.51196695415327,0.527505395662312,
0.535690782065472,0.537747559764025,0.538956555931311,0.540035311791355,
0.54143275341975,0.543765990741589,0.55837822406314,0.566577061161562,0.579798205438069,
0.612654542865741,0.629210578832585,0.639519319013962,0.642767991785144,
0.644841461486117,0.646782398989346,0.649324083771974,0.653620371647605,
0.688792552375121,0.737864776517521,0.747475569035496,0.749640943621061,
0.750874055446313,0.751948321104482,0.753329499684386,0.755557624182768,
0.768034521137767,0.772703615145575,0.823043088942335,0.840662357913241,
0.851445598070382,0.854747754737872,0.856833053483619,0.858769619820171,
0.86128357839281,0.865484378975842,0.895589004174204,0.947253201791336,
0.959259754409079,0.961571364824705,0.962836423381644,0.963907364194148,
0.965244782554016,0.967329069461115,0.977413353750753,0.982911559660835,
0.992300890531631,1.00387203193161,1.036719271018,1.0532606152779,1.06356316211411,
1.06681145690083,1.06888506379014,1.07082639563468,1.07336898061614,1.07766765068432,
1.11297821999515,1.16223323195852,1.17157100098013,1.17371728114146,1.17494630860135,
1.17602142579438,1.17740950961519,1.18031958109539,1.20845096251774,1.24814071125033,
1.26508638309759,1.27557123127229,1.27884050040433,1.28091883356835,1.28285853702239,
1.28539029585084,1.28965127770395,1.33465169887647,1.37970331859847,1.38442858727116,
1.38617091267851,1.38719692087222,1.38828963349461,1.38980016400639,1.39338182821556,
1.40880841792372),.UNSPECIFIED.);
#2007=B_SPLINE_CURVE_WITH_KNOTS('',3,(#197630,#197631,#197632,#197633,#197634),
 .UNSPECIFIED.,.F.,.F.,(4,1,4),(76.7075601022117,76.9104066470643,77.0584304051426),
 .UNSPECIFIED.);
#2008=B_SPLINE_CURVE_WITH_KNOTS('',3,(#197635,#197636,#197637,#197638,#197639,
#197640,#197641,#197642,#197643,#197644,#197645,#197646,#197647,#197648,
#197649,#197650,#197651,#197652,#197653,#197654,#197655,#197656,#197657,
#197658,#197659,#197660,#197661,#197662,#197663,#197664,#197665,#197666,
#197667,#197668,#197669,#197670,#197671,#197672,#197673,#197674,#197675,
#197676,#197677,#197678,#197679,#197680,#197681,#197682,#197683,#197684,
#197685,#197686,#197687,#197688,#197689,#197690,#197691,#197692,#197693,
#197694,#197695,#197696,#197697,#197698,#197699,#197700,#197701,#197702,
#197703,#197704,#197705,#197706,#197707,#197708,#197709,#197710,#197711,
#197712,#197713,#197714,#197715,#197716,#197717,#197718,#197719,#197720,
#197721,#197722,#197723,#197724,#197725,#197726,#197727,#197728,#197729,
#197730,#197731,#197732,#197733,#197734,#197735,#197736,#197737,#197738,
#197739,#197740,#197741,#197742,#197743,#197744,#197745,#197746,#197747,
#197748,#197749,#197750,#197751,#197752,#197753,#197754,#197755,#197756,
#197757,#197758,#197759,#197760,#197761,#197762,#197763,#197764,#197765,
#197766,#197767,#197768,#197769,#197770,#197771,#197772,#197773,#197774,
#197775,#197776,#197777,#197778,#197779,#197780,#197781,#197782,#197783,
#197784,#197785,#197786,#197787,#197788,#197789,#197790,#197791,#197792,
#197793,#197794,#197795,#197796,#197797,#197798,#197799,#197800,#197801,
#197802,#197803,#197804,#197805,#197806,#197807,#197808,#197809,#197810,
#197811,#197812,#197813,#197814,#197815,#197816,#197817,#197818,#197819,
#197820,#197821,#197822,#197823,#197824,#197825,#197826,#197827,#197828,
#197829,#197830,#197831,#197832,#197833,#197834,#197835,#197836,#197837,
#197838,#197839,#197840,#197841,#197842,#197843,#197844,#197845,#197846,
#197847,#197848,#197849,#197850,#197851,#197852,#197853,#197854,#197855,
#197856),.UNSPECIFIED.,.F.,.F.,(4,2,2,2,2,2,2,2,2,2,2,2,2,2,2,2,2,2,2,2,
2,2,2,2,2,2,2,2,2,2,2,2,2,2,2,2,2,2,2,2,2,2,2,2,2,2,2,2,2,2,2,2,2,2,2,2,
2,2,2,2,2,2,2,2,2,2,2,2,2,2,2,2,2,2,2,2,2,2,2,2,2,2,2,2,2,2,2,2,2,2,2,2,
2,2,2,2,2,2,2,2,2,2,2,2,2,2,2,2,2,2,4),(0.000629228676279194,0.0527834506842141,
0.0572122890737632,0.0609073219001442,0.0630791178976013,0.0649948664632921,
0.0673872018486889,0.0710961029451884,0.0893741307873062,0.100875358156077,
0.113855404834142,0.129422626240354,0.154644590672702,0.165757198924741,
0.168025986247171,0.169282505526748,0.170353540664101,0.171700384179906,
0.17431877797379,0.190313594831012,0.19570790421775,0.252779457535905,0.268947752408923,
0.272743940652662,0.274937889759981,0.276850920133946,0.279211074091741,
0.282816168391261,0.299508791647547,0.307019410709072,0.355519527389341,
0.3702513606368,0.378146063753463,0.380177794224394,0.381380972806579,0.382460726930709,
0.383867576065394,0.386233811473231,0.401654125028369,0.405923967024112,
0.448898512719925,0.476830175884744,0.483170369325384,0.485862824672043,
0.48782123787068,0.489616724533124,0.492499090160279,0.499491669635509,
0.551012040718334,0.57803351460542,0.589618494103655,0.591906363351962,
0.593165943163878,0.594236758012706,0.59557973577398,0.598180127255755,
0.613745321169219,0.620203171439649,0.66161261760335,0.688881510204923,
0.695141150523975,0.697819888360012,0.699775924492642,0.701574523450607,
0.704473563607079,0.711565843614122,0.761217898189458,0.799526595823581,
0.803130554894181,0.804644357639806,0.80573715469611,0.806761429207059,
0.808496950401207,0.813181324585151,0.854259244217092,0.900683905985834,
0.907075142276693,0.909776383056871,0.911736477921162,0.91353025530243,
0.916402766768146,0.923334954531907,0.975776204784388,1.00214730968667,
1.01357064115006,1.01584952895468,1.0171072144458,1.01817826251613,1.01952387516536,
1.0221362182242,1.03798592755138,1.04272917970373,1.05800575391191,1.09087775189184,
1.1074576345621,1.11777655337403,1.12102595057109,1.12309928639277,1.12503967987205,
1.12758004828269,1.131872757716,1.17426855659149,1.20332291167791,1.22293675891397,
1.22689151979009,1.22846302273638,1.22956648478356,1.23057684249836,1.23224028131276,
1.236464936696,1.25979359209778),.UNSPECIFIED.);
#2009=B_SPLINE_CURVE_WITH_KNOTS('',3,(#197858,#197859,#197860,#197861,#197862,
#197863,#197864,#197865,#197866,#197867,#197868,#197869,#197870,#197871,
#197872,#197873,#197874,#197875,#197876,#197877,#197878,#197879,#197880,
#197881,#197882,#197883,#197884,#197885,#197886,#197887,#197888,#197889,
#197890,#197891,#197892,#197893,#197894,#197895,#197896,#197897,#197898,
#197899,#197900,#197901,#197902,#197903,#197904,#197905,#197906,#197907,
#197908,#197909,#197910,#197911,#197912,#197913,#197914,#197915,#197916,
#197917,#197918,#197919,#197920,#197921,#197922,#197923,#197924,#197925,
#197926,#197927,#197928,#197929,#197930,#197931,#197932,#197933,#197934,
#197935,#197936,#197937,#197938,#197939,#197940,#197941,#197942,#197943,
#197944,#197945,#197946,#197947,#197948,#197949,#197950,#197951,#197952,
#197953,#197954,#197955,#197956,#197957,#197958,#197959,#197960,#197961,
#197962,#197963,#197964,#197965,#197966,#197967,#197968,#197969,#197970,
#197971,#197972,#197973,#197974,#197975,#197976,#197977,#197978,#197979,
#197980,#197981,#197982,#197983,#197984,#197985,#197986,#197987,#197988,
#197989,#197990,#197991,#197992,#197993,#197994,#197995,#197996,#197997,
#197998,#197999,#198000,#198001,#198002,#198003,#198004,#198005,#198006,
#198007,#198008,#198009,#198010,#198011,#198012,#198013,#198014,#198015,
#198016,#198017,#198018,#198019,#198020,#198021,#198022,#198023,#198024,
#198025,#198026,#198027,#198028,#198029,#198030,#198031,#198032,#198033,
#198034,#198035,#198036,#198037,#198038,#198039,#198040,#198041,#198042,
#198043,#198044,#198045,#198046,#198047,#198048,#198049,#198050,#198051,
#198052,#198053,#198054,#198055,#198056,#198057,#198058,#198059,#198060,
#198061,#198062,#198063,#198064,#198065,#198066,#198067,#198068,#198069,
#198070,#198071,#198072,#198073,#198074,#198075,#198076,#198077,#198078,
#198079,#198080,#198081,#198082,#198083),.UNSPECIFIED.,.F.,.F.,(4,2,2,2,
2,2,2,2,2,2,2,2,2,2,2,2,2,2,2,2,2,2,2,2,2,2,2,2,2,2,2,2,2,2,2,2,2,2,2,2,
2,2,2,2,2,2,2,2,2,2,2,2,2,2,2,2,2,2,2,2,2,2,2,2,2,2,2,2,2,2,2,2,2,2,2,2,
2,2,2,2,2,2,2,2,2,2,2,2,2,2,2,2,2,2,2,2,2,2,2,2,2,2,2,2,2,2,2,2,2,2,2,2,
4),(1.40880841792372,1.43101997011835,1.48144340271669,1.48850203098995,
1.49139648684803,1.49319500633745,1.49515315669075,1.49783876541391,1.5041327669713,
1.5316719318947,1.56007598033247,1.58240616418509,1.59511320409958,1.59735378325235,
1.59873883941128,1.59981366251036,1.60104466340688,1.60319981324344,1.61266153047195,
1.6618473339337,1.69705242112975,1.70134972363743,1.70389199475506,1.70583336105332,
1.70790726954843,1.71115658835216,1.7214669446394,1.73802746971779,1.77091963230637,
1.78465511414046,1.79152685943823,1.79173721671427,1.79510233306198,1.80720789297196,
1.80941609609006,1.81079133466597,1.81186513504218,1.81310241871079,1.81528637014086,
1.82516584462093,1.87399142184213,1.90908129797623,1.91337682220747,1.91591848588703,
1.91785964438777,1.91993357918921,1.92318345766908,1.9334999608329,1.95007451855918,
1.98297698893026,1.9978543197517,2.00287124273322,2.01889450782522,2.02151529739038,
2.02286301703774,2.02393456106175,2.02519146540749,2.02746545797424,2.03879304938004,
2.06477635953734,2.11776185631112,2.12465535076338,2.12752213243445,2.12931533802002,
2.13127722879156,2.13398537144229,2.14041383627185,2.16907359567702,2.22038027673558,
2.23140764499874,2.23355292398433,2.23490902409013,2.23598117748184,2.23723182647198,
2.23947699110722,2.25031485350018,2.27442776711455,2.33017537794966,2.33682517366497,
2.33936873441911,2.34119607934516,2.34313472547635,2.34570543075798,2.35135441365152,
2.37387692992762,2.40662272430839,2.44267392561182,2.44553218269773,2.44691002465133,
2.44794933915377,2.44914452258852,2.45041830743122,2.45235159391131,2.4559278827369,
2.46439798759593,2.52405085558296,2.54591226606874,2.54983010470779,2.55228662601291,
2.5542094882945,2.55634335583337,2.55986527124225,2.57283726665067,2.59578767651268,
2.64810982117262,2.65598082521307,2.65807664894648,2.65930652318843,2.6603632451898,
2.66140905420161,2.66275937318509,2.66521722158727,2.66831062682325),
 .UNSPECIFIED.);
#2010=B_SPLINE_CURVE_WITH_KNOTS('',3,(#198084,#198085,#198086,#198087,#198088,
#198089),.UNSPECIFIED.,.F.,.F.,(4,2,4),(0.000817343676032421,0.0612254265673932,
0.0752219485597137),.UNSPECIFIED.);
#2011=B_SPLINE_CURVE_WITH_KNOTS('',3,(#198095,#198096,#198097,#198098,#198099,
#198100,#198101,#198102,#198103,#198104,#198105,#198106,#198107),
 .UNSPECIFIED.,.F.,.F.,(4,3,3,3,4),(82.9907456874175,83.0928761471927,83.1948834239568,
83.2967928187986,83.3413404565306),.UNSPECIFIED.);
#2012=B_SPLINE_CURVE_WITH_KNOTS('',3,(#198108,#198109,#198110,#198111,#198112,
#198113,#198114,#198115,#198116,#198117),.UNSPECIFIED.,.F.,.F.,(4,1,1,1,
1,1,1,4),(77.0584304051426,77.9092430970262,78.9080795469881,79.9069159969499,
80.9057524469118,81.9045888968737,82.9034253468356,82.9907454093913),
 .UNSPECIFIED.);
#2013=B_SPLINE_CURVE_WITH_KNOTS('',3,(#198118,#198119,#198120,#198121,#198122,
#198123,#198124,#198125,#198126,#198127,#198128,#198129,#198130,#198131,
#198132,#198133,#198134,#198135,#198136,#198137,#198138,#198139,#198140,
#198141,#198142,#198143,#198144,#198145,#198146,#198147,#198148,#198149,
#198150,#198151,#198152,#198153,#198154,#198155,#198156,#198157,#198158,
#198159,#198160,#198161,#198162,#198163,#198164,#198165,#198166,#198167,
#198168,#198169,#198170,#198171,#198172,#198173,#198174,#198175,#198176,
#198177,#198178,#198179,#198180,#198181,#198182,#198183,#198184,#198185,
#198186,#198187,#198188,#198189,#198190,#198191,#198192,#198193,#198194,
#198195,#198196,#198197,#198198,#198199,#198200,#198201,#198202,#198203,
#198204,#198205,#198206,#198207,#198208,#198209,#198210,#198211,#198212,
#198213,#198214,#198215,#198216,#198217,#198218,#198219,#198220,#198221,
#198222,#198223,#198224,#198225,#198226,#198227,#198228,#198229,#198230,
#198231,#198232,#198233,#198234,#198235,#198236,#198237,#198238,#198239,
#198240,#198241,#198242,#198243,#198244,#198245,#198246,#198247,#198248,
#198249,#198250,#198251,#198252,#198253,#198254,#198255,#198256,#198257,
#198258,#198259,#198260,#198261,#198262,#198263,#198264,#198265,#198266,
#198267,#198268,#198269,#198270,#198271,#198272,#198273,#198274,#198275,
#198276,#198277,#198278,#198279,#198280,#198281,#198282,#198283,#198284,
#198285,#198286,#198287,#198288,#198289,#198290,#198291,#198292,#198293,
#198294,#198295,#198296,#198297,#198298,#198299,#198300,#198301,#198302,
#198303,#198304,#198305,#198306,#198307,#198308,#198309,#198310,#198311,
#198312,#198313,#198314,#198315,#198316,#198317,#198318,#198319,#198320,
#198321,#198322,#198323,#198324,#198325,#198326,#198327,#198328,#198329,
#198330,#198331,#198332,#198333,#198334,#198335,#198336,#198337,#198338,
#198339,#198340,#198341,#198342,#198343,#198344,#198345,#198346,#198347,
#198348,#198349,#198350,#198351,#198352,#198353,#198354,#198355,#198356,
#198357,#198358,#198359,#198360,#198361,#198362,#198363,#198364,#198365,
#198366,#198367,#198368,#198369,#198370,#198371,#198372,#198373,#198374,
#198375,#198376,#198377,#198378,#198379,#198380,#198381,#198382,#198383,
#198384,#198385,#198386,#198387),.UNSPECIFIED.,.F.,.F.,(4,2,2,2,2,2,2,2,
2,2,2,2,2,2,2,2,2,2,2,2,2,2,2,2,2,2,2,2,2,2,2,2,2,2,2,2,2,2,2,2,2,2,2,2,
2,2,2,2,2,2,2,2,2,2,2,2,2,2,2,2,2,2,2,2,2,2,2,2,2,2,2,2,2,2,2,2,2,2,2,2,
2,2,2,2,2,2,2,2,2,2,2,2,2,2,2,2,2,2,2,2,2,2,2,2,2,2,2,2,2,2,2,2,2,2,2,2,
2,2,2,2,2,2,2,2,2,2,2,2,2,2,2,2,2,2,4),(0.0752219485597137,0.0876737733029266,
0.0938318777926784,0.0964929851085831,0.0984458590727868,0.100248364936695,
0.103168891336402,0.110389684477826,0.154249330517679,0.195394745934447,
0.199213040908045,0.201237857018698,0.2025493772978,0.203773004267836,0.203776571015409,
0.203780150357518,0.203783742356241,0.203787580102183,0.203791479604201,
0.203795442215694,0.203799469200582,0.203803562193082,0.203807722511776,
0.203811951609945,0.203816250925197,0.203820621936599,0.203825066484,0.203829586160866,
0.203834182563694,0.203838857492989,0.203843612621636,0.203848449836046,
0.204892179818097,0.206274880308293,0.209159666278352,0.243328974195012,
0.27757081259187,0.294125489025972,0.30443276469162,0.307680647015343,0.309753533172861,
0.311693868908419,0.314234685553496,0.318529326413003,0.353664018923092,
0.402636125373647,0.412344052578725,0.414515702355721,0.41574996653691,
0.416823681212764,0.418202116159678,0.421064705760515,0.45673982715691,
0.489566236134306,0.506090988429658,0.516384984815751,0.51963153449997,
0.521704256101316,0.523644919890115,0.526186861985578,0.5304849656276,0.565866214730676,
0.615040069717612,0.624354377622764,0.626498422545301,0.627726677807272,
0.628801450447854,0.630189525985197,0.633101119278578,0.664540225858998,
0.715320677188441,0.72791257676452,0.731398750354841,0.733524475083077,
0.735448754805604,0.737919265477722,0.741884064547403,0.76485918052092,
0.823420483458493,0.836039021492217,0.838381978493775,0.839653663194521,
0.840724022450337,0.842052962543649,0.844110099785209,0.8538100709527,0.859594247613297,
0.860030125278103,0.866915603183283,0.880642879647557,0.913503964103421,
0.930065916623037,0.940377309841268,0.943626270016112,0.945699791319999,
0.94764068452207,0.95018217767509,0.954477842139657,0.989605027864029,1.03853647933468,
1.0483122506774,1.05048899500394,1.0517246010037,1.05279848804178,1.05417584379465,
1.05703171390351,1.07981293386321,1.09265757223245,1.12551358123912,1.14206696315663,
1.15237477849041,1.15562354724399,1.15769717133001,1.15963831877472,1.1621803728906,
1.16647749671,1.20168515380954,1.25086767596654,1.26035706105177,1.26251406211317,
1.26374540444121,1.26482006731463,1.26620430415427,1.26909488658854,1.29479851747829,
1.33424611894595,1.36197018183995,1.3661108826407,1.36860741670612,1.37054151261102,
1.37263503959985,1.37597366853975,1.38709012111101,1.4054761068303,1.40869849150873),
 .UNSPECIFIED.);
#2014=B_SPLINE_CURVE_WITH_KNOTS('',3,(#198393,#198394,#198395,#198396,#198397,
#198398,#198399,#198400,#198401,#198402,#198403,#198404,#198405,#198406,
#198407,#198408,#198409,#198410,#198411,#198412,#198413,#198414,#198415,
#198416,#198417,#198418),.UNSPECIFIED.,.F.,.F.,(4,2,2,2,2,2,2,2,2,2,2,2,
4),(2.59385173281912,2.61315066313481,2.62526726593595,2.62709460362196,
2.62809611461634,2.63678412524615,2.63993532549552,2.64178241720017,2.64363741504273,
2.64550551036064,2.6479070159309,2.65164701932836,2.66828059292683),
 .UNSPECIFIED.);
#2015=B_SPLINE_CURVE_WITH_KNOTS('',3,(#198419,#198420,#198421,#198422,#198423,
#198424,#198425,#198426,#198427,#198428,#198429,#198430,#198431,#198432,
#198433,#198434,#198435,#198436,#198437,#198438,#198439,#198440,#198441,
#198442,#198443,#198444,#198445,#198446,#198447,#198448,#198449,#198450,
#198451,#198452,#198453,#198454,#198455,#198456,#198457,#198458,#198459,
#198460,#198461,#198462,#198463,#198464,#198465,#198466,#198467,#198468,
#198469,#198470,#198471,#198472,#198473,#198474,#198475,#198476,#198477,
#198478,#198479,#198480,#198481,#198482,#198483,#198484,#198485,#198486,
#198487,#198488,#198489,#198490,#198491,#198492,#198493,#198494,#198495,
#198496,#198497,#198498,#198499,#198500,#198501,#198502,#198503,#198504,
#198505,#198506,#198507,#198508,#198509,#198510,#198511,#198512,#198513,
#198514,#198515,#198516,#198517,#198518,#198519,#198520,#198521,#198522,
#198523,#198524,#198525,#198526,#198527,#198528,#198529,#198530,#198531,
#198532,#198533,#198534,#198535,#198536,#198537,#198538,#198539,#198540,
#198541,#198542,#198543,#198544,#198545,#198546,#198547,#198548,#198549,
#198550,#198551,#198552,#198553,#198554,#198555,#198556,#198557,#198558,
#198559,#198560,#198561,#198562,#198563,#198564,#198565,#198566,#198567,
#198568,#198569,#198570,#198571,#198572,#198573,#198574,#198575,#198576,
#198577,#198578,#198579,#198580,#198581,#198582,#198583,#198584,#198585,
#198586,#198587,#198588,#198589,#198590,#198591,#198592,#198593,#198594,
#198595,#198596,#198597,#198598,#198599),.UNSPECIFIED.,.F.,.F.,(4,3,3,3,
3,3,3,3,3,3,3,3,3,3,3,3,3,3,3,3,3,3,3,3,3,3,3,3,3,3,3,3,3,3,3,3,3,3,3,3,
3,3,3,3,3,3,3,3,3,3,3,3,3,3,3,3,3,3,3,3,4),(83.3413404565306,83.4431911419029,
83.5450420266759,83.6469948978629,83.7490046894964,83.851187834397,83.9022617967974,
84.0056565338452,84.1088978159599,84.2120177813522,84.315072349561,84.4180955579187,
84.5211214005913,84.6242541673693,84.7274432587791,84.8308152521607,84.9010982467593,
85.0044929838072,85.1077342659224,85.2108542313147,85.3139087995236,85.4169320078813,
85.5199578505538,85.6230906173319,85.7262797087417,85.8296517021233,85.8999346967212,
86.0033294337692,86.1065707158841,86.2096906812764,86.3127452494853,86.415768457843,
86.5187943005157,86.6219270672937,86.7251161587035,86.8284881520851,86.8987711466831,
87.0021658837311,87.105407165846,87.2085271312382,87.3115816994471,87.4146049078047,
87.5176307504776,87.6207635172557,87.7239526086653,87.8273246020469,87.8976075966449,
88.0010023336929,88.1042436158077,88.2073635811999,88.3104181494089,88.4134413577665,
88.516467200439,88.6195999672169,88.7227890586267,88.8261610520084,88.8964440466068,
89.0132269961633,89.129558683076,89.245139987838,89.2739307161836),
 .UNSPECIFIED.);
#2016=B_SPLINE_CURVE_WITH_KNOTS('',3,(#198601,#198602,#198603,#198604,#198605,
#198606,#198607,#198608,#198609,#198610,#198611,#198612,#198613,#198614,
#198615,#198616,#198617,#198618,#198619,#198620,#198621,#198622,#198623,
#198624,#198625,#198626,#198627,#198628,#198629,#198630,#198631,#198632,
#198633,#198634,#198635,#198636,#198637,#198638,#198639,#198640,#198641,
#198642,#198643,#198644,#198645,#198646,#198647,#198648,#198649,#198650,
#198651,#198652,#198653,#198654,#198655,#198656,#198657,#198658,#198659,
#198660,#198661,#198662,#198663,#198664,#198665,#198666,#198667,#198668,
#198669,#198670,#198671,#198672,#198673,#198674,#198675,#198676,#198677,
#198678,#198679,#198680,#198681,#198682,#198683,#198684,#198685,#198686,
#198687,#198688,#198689,#198690,#198691,#198692,#198693,#198694,#198695,
#198696,#198697,#198698,#198699,#198700,#198701,#198702,#198703,#198704,
#198705,#198706,#198707,#198708,#198709,#198710,#198711,#198712,#198713,
#198714,#198715,#198716,#198717,#198718,#198719,#198720,#198721,#198722,
#198723,#198724,#198725,#198726,#198727,#198728,#198729,#198730,#198731,
#198732,#198733,#198734,#198735,#198736,#198737,#198738,#198739,#198740,
#198741,#198742,#198743,#198744,#198745,#198746,#198747,#198748,#198749,
#198750,#198751,#198752,#198753,#198754,#198755,#198756,#198757,#198758,
#198759,#198760,#198761,#198762,#198763,#198764,#198765,#198766,#198767,
#198768,#198769,#198770,#198771,#198772,#198773,#198774,#198775,#198776,
#198777,#198778,#198779,#198780,#198781,#198782,#198783,#198784,#198785,
#198786,#198787,#198788,#198789,#198790,#198791,#198792,#198793,#198794,
#198795,#198796,#198797,#198798,#198799,#198800,#198801,#198802,#198803,
#198804,#198805,#198806,#198807,#198808,#198809,#198810,#198811,#198812,
#198813,#198814,#198815,#198816,#198817,#198818,#198819,#198820,#198821,
#198822,#198823,#198824,#198825,#198826,#198827,#198828),.UNSPECIFIED.,
 .F.,.F.,(4,2,2,2,2,2,2,2,2,2,2,2,2,2,2,2,2,2,2,2,2,2,2,2,2,2,2,2,2,2,2,
2,2,2,2,2,2,2,2,2,2,2,2,2,2,2,2,2,2,2,2,2,2,2,2,2,2,2,2,2,2,2,2,2,2,2,2,
2,2,2,2,2,2,2,2,2,2,2,2,2,2,2,2,2,2,2,2,2,2,2,2,2,2,2,2,2,2,2,2,2,2,2,2,
2,2,2,2,2,2,2,2,2,2,4),(1.40869849150873,1.45282999451277,1.47139320436944,
1.47413964982754,1.4754954227699,1.47656762600383,1.47781868811996,1.48006548139551,
1.49092827283456,1.51513260841594,1.5557644112509,1.57472007913753,1.57847476178802,
1.58088182783535,1.58279981247997,1.58496394597157,1.58862108920682,1.60315630343547,
1.63041105310353,1.67885590606411,1.68487399554867,1.6867933446037,1.68797195217562,
1.68906063826672,1.69054748325081,1.69399238118545,1.69876842221026,1.71159051457192,
1.75729466100386,1.78601286148282,1.79018013714976,1.79268458549216,1.79462002923047,
1.79671026364585,1.80003340912451,1.81100424264699,1.82905329556861,1.87930839629007,
1.8853934510873,1.89613523163867,1.89826280713267,1.89961363106515,1.90068558746215,
1.90194059826735,1.90420514712472,1.91536385835007,1.9406865562147,1.99464856661658,
2.00146566612399,2.00432022060142,2.00611147851677,2.00807584100176,2.01079586987848,
2.01729299201516,2.04652667672953,2.08228004942426,2.09145789885947,2.10770424299693,
2.11033421361682,2.1116840227843,2.11275584801668,2.11401148510361,2.11627913667979,
2.12749284169255,2.15302910826818,2.20667365531364,2.21351662363869,2.21637534133464,
2.21816727041529,2.22013080194248,2.22284679400517,2.22932047284512,2.2836635842511,
2.28607016932554,2.30397872243829,2.31983135887965,2.32244507202444,2.323791374139,
2.32486296197884,2.32612127644059,2.32840128113389,2.33983030250532,2.36621192370692,
2.41864182465004,2.42557719298027,2.42845110295001,2.43024577948122,2.43216758461202,
2.43478026075135,2.43770639068747,2.44271806203508,2.45338552959112,2.48461083736921,
2.52889863931077,2.53356177346718,2.53529459443978,2.53631869273946,2.53741251089712,
2.53892970481681,2.54255092618303,2.54764383670332,2.56173527925422,2.61338515130572,
2.62550364419783,2.62733126705756,2.62833293305939,2.63702229924639,2.64017399109347,
2.64202137093178,2.64387665813868,2.64574504485191,2.64814692501092,2.65188751176353,
2.6685236796344),.UNSPECIFIED.);
#2017=B_SPLINE_CURVE_WITH_KNOTS('',3,(#198829,#198830,#198831,#198832,#198833,
#198834,#198835,#198836,#198837,#198838),.UNSPECIFIED.,.F.,.F.,(4,3,3,4),
(-85.8723819380379,-85.7556990039215,-85.6390735155331,-85.5224480271446),
 .UNSPECIFIED.);
#2018=B_SPLINE_CURVE_WITH_KNOTS('',3,(#198843,#198844,#198845,#198846,#198847,
#198848,#198849,#198850,#198851,#198852,#198853,#198854,#198855,#198856,
#198857,#198858,#198859,#198860,#198861,#198862,#198863,#198864,#198865,
#198866,#198867,#198868,#198869,#198870,#198871,#198872,#198873,#198874,
#198875,#198876,#198877,#198878,#198879,#198880,#198881,#198882,#198883,
#198884,#198885,#198886,#198887,#198888,#198889,#198890,#198891,#198892,
#198893,#198894,#198895,#198896,#198897,#198898,#198899,#198900,#198901,
#198902,#198903,#198904,#198905,#198906,#198907,#198908,#198909,#198910,
#198911,#198912,#198913,#198914,#198915,#198916,#198917,#198918,#198919,
#198920,#198921,#198922,#198923,#198924,#198925,#198926,#198927,#198928,
#198929,#198930,#198931,#198932,#198933,#198934,#198935,#198936,#198937,
#198938,#198939,#198940,#198941,#198942,#198943,#198944,#198945,#198946,
#198947,#198948,#198949,#198950,#198951,#198952,#198953,#198954,#198955,
#198956,#198957,#198958,#198959,#198960,#198961,#198962,#198963,#198964,
#198965,#198966,#198967,#198968,#198969,#198970,#198971,#198972,#198973,
#198974,#198975,#198976,#198977,#198978,#198979,#198980,#198981,#198982,
#198983,#198984,#198985,#198986,#198987,#198988,#198989,#198990,#198991,
#198992,#198993,#198994,#198995,#198996,#198997,#198998,#198999,#199000,
#199001,#199002,#199003,#199004,#199005,#199006,#199007,#199008,#199009,
#199010,#199011,#199012,#199013,#199014,#199015,#199016,#199017,#199018,
#199019,#199020,#199021,#199022,#199023,#199024,#199025,#199026,#199027,
#199028,#199029,#199030,#199031,#199032,#199033,#199034,#199035,#199036,
#199037,#199038,#199039,#199040,#199041,#199042,#199043,#199044,#199045,
#199046,#199047,#199048,#199049,#199050,#199051,#199052,#199053,#199054,
#199055,#199056,#199057,#199058,#199059,#199060,#199061,#199062,#199063,
#199064,#199065,#199066,#199067,#199068,#199069,#199070,#199071,#199072,
#199073,#199074,#199075,#199076),.UNSPECIFIED.,.F.,.F.,(4,2,2,2,2,2,2,2,
2,2,2,2,2,2,2,2,2,2,2,2,2,2,2,2,2,2,2,2,2,2,2,2,2,2,2,2,2,2,2,2,2,2,2,2,
2,2,2,2,2,2,2,2,2,2,2,2,2,2,2,2,2,2,2,2,2,2,2,2,2,2,2,2,2,2,2,2,2,2,2,2,
2,2,2,2,2,2,2,2,2,2,2,2,2,2,2,2,2,2,2,2,2,2,2,2,2,2,2,2,2,2,2,2,2,2,2,2,
4),(1.26008679584093,1.2603413105264,1.26249802864315,1.26372920944908,
1.26480373135215,1.26618778661088,1.2690779898589,1.29477824700187,1.3342206771408,
1.36194110379178,1.36608126145692,1.36857746804445,1.37051131024333,1.37260456260776,
1.37594275358238,1.38705774777023,1.40544132125641,1.45278900991273,1.47134977490511,
1.47409585979184,1.47545145482721,1.47652351740771,1.47777441545709,1.48002091420739,
1.4908822840175,1.51508345677271,1.55570992129749,1.57466309758851,1.57841728731957,
1.58082403749609,1.58274177053474,1.5849056202199,1.58856228407212,1.60309559589524,
1.63034678272025,1.67878538567897,1.68480258921642,1.68672167451692,1.68790012481218,
1.68898866915346,1.69047532557243,1.69391980857443,1.71499919649434,1.75523958959363,
1.78583819386779,1.79005036886686,1.79256780132352,1.79450508384327,1.79658922337749,
1.79988543356867,1.81061260261821,1.82810633394543,1.87781222265419,1.89544518422071,
1.89812709711412,1.89948798428238,1.9005605708405,1.9018078838582,1.90403752821918,
1.91462094565197,1.93780182652106,1.99499600940796,2.00149099514587,2.00400988944245,
2.00583081917494,2.00777314725302,2.01036673091977,2.01614041302495,2.03959180885092,
2.08393330297765,2.10728335130664,2.11014619447026,2.11152499875734,2.11259911362248,
2.11383397325131,2.11600698016759,2.12572639757834,2.17468533809976,2.20983460356922,
2.21412171957463,2.21666091332031,2.21860163017905,2.22067649562734,2.22393076493239,
2.23428600884851,2.25094648885346,2.2839198252524,2.30291616025821,2.30400226766826,
2.31965431988133,2.32226135506949,2.32360609237969,2.32467742555796,2.32593659224789,
2.32822108271443,2.33973407961209,2.36645438123486,2.41839183487559,2.42535909431864,
2.42823799163131,2.43003337632152,2.4319540526298,2.43456182748373,2.43748124032635,
2.44247667344687,2.4530966500259,2.48435517938215,2.52866826149156,2.53333737182369,
2.53507094185315,2.53609508012374,2.53718859750785,2.53870481229946,2.54232108570804,
2.54740525298321,2.56146200600718,2.59385173281912),.UNSPECIFIED.);
#2019=B_SPLINE_CURVE_WITH_KNOTS('',3,(#199078,#199079,#199080,#199081,#199082,
#199083,#199084,#199085,#199086,#199087,#199088,#199089,#199090,#199091,
#199092,#199093,#199094,#199095,#199096,#199097,#199098,#199099,#199100,
#199101,#199102,#199103,#199104,#199105,#199106,#199107,#199108,#199109,
#199110,#199111,#199112,#199113,#199114,#199115,#199116,#199117,#199118,
#199119,#199120,#199121,#199122,#199123,#199124,#199125,#199126,#199127,
#199128,#199129,#199130,#199131,#199132,#199133,#199134,#199135,#199136,
#199137,#199138,#199139,#199140,#199141,#199142,#199143,#199144,#199145,
#199146,#199147,#199148,#199149,#199150,#199151,#199152,#199153,#199154,
#199155,#199156,#199157,#199158,#199159,#199160,#199161,#199162,#199163,
#199164,#199165,#199166,#199167,#199168,#199169,#199170,#199171,#199172,
#199173,#199174,#199175,#199176,#199177,#199178,#199179,#199180,#199181,
#199182,#199183,#199184,#199185,#199186,#199187,#199188,#199189,#199190,
#199191,#199192,#199193,#199194,#199195,#199196,#199197,#199198,#199199,
#199200,#199201,#199202,#199203,#199204,#199205,#199206,#199207,#199208,
#199209,#199210,#199211,#199212,#199213,#199214,#199215,#199216,#199217,
#199218,#199219,#199220,#199221,#199222,#199223,#199224,#199225,#199226,
#199227,#199228,#199229,#199230,#199231,#199232,#199233,#199234,#199235,
#199236,#199237,#199238,#199239,#199240,#199241,#199242,#199243,#199244,
#199245,#199246,#199247,#199248,#199249,#199250,#199251,#199252,#199253,
#199254,#199255,#199256,#199257,#199258),.UNSPECIFIED.,.F.,.F.,(4,3,3,3,
3,3,3,3,3,3,3,3,3,3,3,3,3,3,3,3,3,3,3,3,3,3,3,3,3,3,3,3,3,3,3,3,3,3,3,3,
3,3,3,3,3,3,3,3,3,3,3,3,3,3,3,3,3,3,3,3,4),(-91.8056330559093,-91.7034783920339,
-91.6014794906741,-91.4995669524681,-91.3977052133587,-91.295858778697,
-91.1939207704756,-91.0919397623156,-90.9897717066845,-90.8941169465305,
-90.7907222094827,-90.6874809273677,-90.5843609619754,-90.4813063937665,
-90.3782831854088,-90.2752573427366,-90.1721245759585,-90.0689354845488,
-89.9655634911672,-89.8952804965687,-89.7918857595209,-89.6886444774058,
-89.5855245120135,-89.4824699438045,-89.3794467354468,-89.2764208927742,
-89.1732881259961,-89.0700990345864,-88.9667270412048,-88.8964440466068,
-88.7930493095588,-88.689808027444,-88.5866880620518,-88.4836334938429,
-88.3806102854851,-88.2775844428123,-88.1744516760342,-88.0712625846243,
-87.9678905912427,-87.8976075966449,-87.7942128595969,-87.690971577482,
-87.5878516120897,-87.4847970438807,-87.3817738355228,-87.2787479928502,
-87.1756152260721,-87.0724261346624,-86.9690541412807,-86.898771146683,
-86.795376409635,-86.6921351275196,-86.5890151621273,-86.4859605939185,
-86.3829373855607,-86.2799115428881,-86.17677877611,-86.0735896847,-85.9702176913185,
-85.8999346967211,-85.8723819380379),.UNSPECIFIED.);
#2020=B_SPLINE_CURVE_WITH_KNOTS('',3,(#199259,#199260,#199261,#199262,#199263),
 .UNSPECIFIED.,.F.,.F.,(4,1,4),(-92.1566392082287,-91.8929533964924,-91.8056333339369),
 .UNSPECIFIED.);
#2021=B_SPLINE_CURVE_WITH_KNOTS('',3,(#199269,#199270,#199271,#199272,#199273,
#199274,#199275,#199276,#199277,#199278,#199279,#199280,#199281,#199282,
#199283,#199284,#199285,#199286,#199287,#199288,#199289,#199290),
 .UNSPECIFIED.,.F.,.F.,(4,2,2,2,2,2,2,2,2,2,4),(2.59411274951175,2.59558337459403,
2.64820215244959,2.65607324743657,2.65816909558666,2.65939898408976,2.66045571833172,
2.66150153941828,2.66285187396475,2.66530975094863,2.66840319211896),
 .UNSPECIFIED.);
#2022=B_SPLINE_CURVE_WITH_KNOTS('',3,(#199291,#199292,#199293,#199294,#199295,
#199296,#199297,#199298,#199299,#199300,#199301,#199302,#199303,#199304,
#199305,#199306,#199307,#199308,#199309,#199310,#199311,#199312,#199313,
#199314,#199315,#199316,#199317,#199318,#199319,#199320,#199321,#199322,
#199323,#199324,#199325,#199326,#199327,#199328,#199329,#199330,#199331,
#199332,#199333,#199334,#199335,#199336,#199337,#199338,#199339,#199340,
#199341,#199342,#199343,#199344,#199345,#199346,#199347,#199348,#199349,
#199350,#199351,#199352,#199353,#199354,#199355,#199356,#199357,#199358,
#199359,#199360,#199361,#199362,#199363,#199364,#199365,#199366,#199367,
#199368,#199369,#199370,#199371,#199372,#199373,#199374,#199375,#199376,
#199377,#199378,#199379,#199380,#199381,#199382,#199383,#199384,#199385,
#199386,#199387,#199388,#199389,#199390,#199391,#199392,#199393,#199394,
#199395,#199396,#199397,#199398,#199399,#199400,#199401,#199402,#199403,
#199404,#199405,#199406,#199407,#199408,#199409,#199410,#199411,#199412,
#199413,#199414,#199415,#199416,#199417,#199418,#199419,#199420,#199421,
#199422,#199423,#199424,#199425,#199426,#199427,#199428,#199429,#199430,
#199431,#199432,#199433,#199434,#199435,#199436,#199437,#199438,#199439,
#199440,#199441,#199442,#199443,#199444,#199445,#199446,#199447,#199448,
#199449,#199450,#199451,#199452,#199453,#199454,#199455,#199456,#199457,
#199458,#199459,#199460,#199461,#199462,#199463,#199464,#199465,#199466,
#199467,#199468,#199469,#199470,#199471,#199472,#199473,#199474,#199475,
#199476,#199477,#199478,#199479,#199480,#199481,#199482,#199483,#199484,
#199485,#199486,#199487,#199488,#199489,#199490,#199491,#199492,#199493,
#199494,#199495,#199496,#199497,#199498,#199499,#199500,#199501,#199502,
#199503,#199504,#199505,#199506,#199507,#199508,#199509,#199510,#199511,
#199512,#199513,#199514,#199515,#199516,#199517,#199518,#199519,#199520,
#199521,#199522,#199523,#199524,#199525,#199526),.UNSPECIFIED.,.F.,.F.,
(4,2,2,2,2,2,2,2,2,2,2,2,2,2,2,2,2,2,2,2,2,2,2,2,2,2,2,2,2,2,2,2,2,2,2,
2,2,2,2,2,2,2,2,2,2,2,2,2,2,2,2,2,2,2,2,2,2,2,2,2,2,2,2,2,2,2,2,2,2,2,2,
2,2,2,2,2,2,2,2,2,2,2,2,2,2,2,2,2,2,2,2,2,2,2,2,2,2,2,2,2,2,2,2,2,2,2,2,
2,2,2,2,2,2,2,2,2,2,4),(0.000817343104692811,0.0612264047101083,0.0876739253814859,
0.0938319268654868,0.0964930162299291,0.098445887033816,0.100248397018484,
0.103168945834367,0.110389872091982,0.154219030417253,0.195392564819818,
0.199211984485171,0.201237223955867,0.202548919747056,0.203772670562241,
0.203776236263053,0.203779814524098,0.20378340541055,0.203787237992897,
0.203791132332205,0.203795089702009,0.203799111357241,0.203803198731046,
0.203807353328477,0.203811576507947,0.203815869861654,0.203820234884912,
0.203824673218311,0.20382918641534,0.20383377623661,0.204877042706698,0.206251542867918,
0.209094350699173,0.231552325634205,0.272263518415933,0.29947632210628,
0.305729177081129,0.308406798604377,0.310362684358796,0.312161608637725,
0.315062199518276,0.322163428537016,0.37162248936672,0.410140140515592,
0.413726291685597,0.415237092776774,0.41632939331663,0.41735453176652,0.419094348826339,
0.42380681086065,0.464614149582666,0.511274379443645,0.517666451742583,
0.520367885181392,0.522328061222922,0.524121872451105,0.526994349817061,
0.533925999287603,0.586379560045428,0.612743989316309,0.624165792435812,
0.626444644865933,0.627702346735141,0.628773430477803,0.630119115555004,
0.632731680126114,0.648588061810793,0.653230360564274,0.711106002460536,
0.727399678916953,0.731188904258926,0.733381484591536,0.735294899668541,
0.73765755804755,0.741270258057818,0.75806104322685,0.765486199005169,0.823507764376126,
0.836082559142699,0.838423097235704,0.839694161009163,0.840764403263711,
0.842093705700601,0.844152313225193,0.853875391593583,0.859629710644237,
0.860066731061031,0.866951568986201,0.880676935212725,0.913533708533091,
0.930093487515048,0.940403527685748,0.943652061627753,0.945725310926782,
0.947665949537185,0.950207109337411,0.95450221041078,0.989624794075012,
1.03854983994315,1.04832431369406,1.05050077144486,1.05173621513491,1.05280996133788,
1.05418713675854,1.05704263399532,1.07982093558274,1.09266381887799,1.12551551786689,
1.14206672793493,1.15237319094318,1.15562153351618,1.15769488558872,1.15963577840455,
1.16217749907585,1.16647405925301,1.20167709949866,1.2508531702071,1.26008679584093),
 .UNSPECIFIED.);
#2023=B_SPLINE_CURVE_WITH_KNOTS('',3,(#199528,#199529,#199530,#199531,#199532,
#199533,#199534,#199535,#199536,#199537),.UNSPECIFIED.,.F.,.F.,(4,1,1,1,
1,1,1,4),(-98.0888186411165,-97.8859720962637,-96.8871356463018,-95.8882991963399,
-94.889462746378,-93.8906262964161,-92.8917898464543,-92.1566392082287),
 .UNSPECIFIED.);
#2024=B_SPLINE_CURVE_WITH_KNOTS('',3,(#199538,#199539,#199540,#199541,#199542,
#199543,#199544,#199545,#199546,#199547,#199548,#199549,#199550,#199551,
#199552,#199553,#199554,#199555,#199556,#199557),.UNSPECIFIED.,.F.,.F.,
(4,2,2,2,2,2,2,2,2,4),(0.000629224934217057,0.0465168723163532,0.0540117796467721,
0.0579010153661128,0.0612291109511265,0.0633196903264559,0.0652535612880513,
0.0677533146320536,0.0719070152574981,0.0751024976388681),.UNSPECIFIED.);
#2025=B_SPLINE_CURVE_WITH_KNOTS('',3,(#199562,#199563,#199564,#199565,#199566,
#199567,#199568,#199569,#199570,#199571,#199572,#199573,#199574,#199575,
#199576,#199577,#199578,#199579,#199580,#199581,#199582,#199583,#199584,
#199585,#199586,#199587,#199588,#199589,#199590,#199591,#199592,#199593,
#199594,#199595,#199596,#199597,#199598,#199599,#199600,#199601,#199602,
#199603,#199604,#199605,#199606,#199607,#199608,#199609,#199610,#199611,
#199612,#199613,#199614,#199615,#199616,#199617,#199618,#199619,#199620,
#199621,#199622,#199623,#199624,#199625,#199626,#199627,#199628,#199629,
#199630,#199631,#199632,#199633,#199634,#199635,#199636,#199637,#199638,
#199639,#199640,#199641,#199642,#199643,#199644,#199645,#199646,#199647,
#199648,#199649,#199650,#199651,#199652,#199653,#199654,#199655,#199656,
#199657,#199658,#199659,#199660,#199661,#199662,#199663,#199664,#199665,
#199666,#199667,#199668,#199669,#199670,#199671,#199672,#199673,#199674,
#199675,#199676,#199677,#199678,#199679,#199680,#199681,#199682,#199683,
#199684,#199685,#199686,#199687,#199688,#199689,#199690,#199691,#199692,
#199693,#199694,#199695,#199696,#199697,#199698,#199699,#199700,#199701,
#199702,#199703,#199704,#199705,#199706,#199707,#199708,#199709,#199710,
#199711,#199712,#199713,#199714,#199715,#199716,#199717,#199718,#199719,
#199720,#199721,#199722,#199723,#199724,#199725,#199726,#199727,#199728,
#199729,#199730,#199731,#199732,#199733,#199734,#199735,#199736,#199737,
#199738,#199739,#199740,#199741,#199742,#199743,#199744,#199745,#199746,
#199747,#199748,#199749,#199750,#199751,#199752,#199753,#199754,#199755,
#199756,#199757,#199758,#199759,#199760,#199761,#199762,#199763,#199764,
#199765,#199766,#199767,#199768,#199769,#199770,#199771,#199772,#199773,
#199774,#199775,#199776,#199777,#199778,#199779,#199780,#199781,#199782,
#199783,#199784,#199785,#199786,#199787,#199788,#199789,#199790,#199791,
#199792,#199793,#199794,#199795,#199796,#199797,#199798,#199799),
 .UNSPECIFIED.,.F.,.F.,(4,2,2,2,2,2,2,2,2,2,2,2,2,2,2,2,2,2,2,2,2,2,2,2,
2,2,2,2,2,2,2,2,2,2,2,2,2,2,2,2,2,2,2,2,2,2,2,2,2,2,2,2,2,2,2,2,2,2,2,2,
2,2,2,2,2,2,2,2,2,2,2,2,2,2,2,2,2,2,2,2,2,2,2,2,2,2,2,2,2,2,2,2,2,2,2,2,
2,2,2,2,2,2,2,2,2,2,2,2,2,2,2,2,2,2,2,2,2,2,4),(1.26019912898447,1.26516552744649,
1.27565047414906,1.27891977403079,1.28099812674898,1.28293784845713,1.28546963111691,
1.28973065308912,1.33473149857969,1.37978354292382,1.38450885614848,1.38625119796463,
1.38727721581579,1.3883699387183,1.38988048343202,1.39346218127488,1.43110066479073,
1.48152458713467,1.48858328117212,1.49147776415741,1.49327630055056,1.49523446934483,
1.49792010342713,1.50421416472924,1.53175359299828,1.56015790678291,1.58248829887166,
1.59519545881556,1.59743605907672,1.59882112827533,1.59989596148789,1.60112697396055,
1.60328214404654,1.61274394989476,1.66193021659652,1.69713563666701,1.70143297964506,
1.703975274694,1.70591665926005,1.70799058726325,1.71123993661749,1.72155038971792,
1.73811107015389,1.77100354210081,1.78473908951812,1.7916110515609,1.79182202413196,
1.79520272497235,1.80729365920458,1.80950106961012,1.8108760751632,1.81194986281409,
1.81318732329243,1.81537204712466,1.8252627572925,1.87407949047141,1.90916655087235,
1.91346207371923,1.91600374925331,1.91794492410745,1.92001888345942,1.92326881519186,
1.93358561205764,1.95016076026618,1.98306390245923,1.99797142940292,2.00296893744556,
2.01898174083656,2.02160193856687,2.02294953815711,2.02402108365242,2.0252781020688,
2.02755258658585,2.03888848731206,2.06490428416925,2.11784401249317,2.12474108952783,
2.12760847672961,2.12940180431983,2.13136362222565,2.13407128599487,2.1404968231754,
2.16913178685335,2.22043122728788,2.23149183504546,2.23363918612668,2.23499592480715,
2.2360681352172,2.2373183358121,2.23956141075427,2.25036457564538,2.27434880313221,
2.33029315208289,2.33692315238296,2.33946362183626,2.34129016054295,2.34322925368523,
2.3458027683106,2.35146696216876,2.37410175434962,2.40691975477404,2.44275877922739,
2.44562069758294,2.44699926424349,2.44803877475975,2.44923356683259,2.45050679225612,
2.45243871827031,2.45601143638465,2.46446957027703,2.52388921598066,2.54598478691587,
2.54991219363759,2.55237162506368,2.55429484554131,2.55642714249414,2.55994191654172,
2.57283594732367,2.59411274951175),.UNSPECIFIED.);
#2026=B_SPLINE_CURVE_WITH_KNOTS('',3,(#199800,#199801,#199802,#199803,#199804,
#199805,#199806,#199807,#199808,#199809,#199810,#199811,#199812,#199813,
#199814,#199815,#199816,#199817,#199818,#199819,#199820,#199821,#199822,
#199823,#199824,#199825,#199826,#199827,#199828,#199829,#199830,#199831,
#199832,#199833,#199834,#199835,#199836,#199837,#199838,#199839,#199840,
#199841,#199842,#199843,#199844,#199845,#199846,#199847,#199848,#199849,
#199850,#199851,#199852,#199853,#199854,#199855,#199856,#199857,#199858,
#199859,#199860,#199861,#199862,#199863,#199864,#199865,#199866,#199867,
#199868,#199869,#199870,#199871,#199872,#199873,#199874,#199875,#199876,
#199877,#199878,#199879,#199880,#199881,#199882,#199883,#199884,#199885,
#199886,#199887,#199888,#199889,#199890,#199891,#199892,#199893,#199894,
#199895,#199896,#199897,#199898,#199899,#199900,#199901,#199902,#199903,
#199904,#199905,#199906,#199907,#199908,#199909,#199910,#199911,#199912,
#199913,#199914,#199915,#199916,#199917,#199918,#199919,#199920,#199921,
#199922,#199923,#199924,#199925,#199926,#199927,#199928,#199929,#199930,
#199931,#199932,#199933,#199934,#199935,#199936,#199937,#199938,#199939,
#199940,#199941,#199942,#199943,#199944,#199945,#199946,#199947,#199948,
#199949,#199950,#199951,#199952,#199953,#199954,#199955,#199956,#199957,
#199958,#199959,#199960,#199961,#199962,#199963,#199964,#199965,#199966,
#199967,#199968,#199969,#199970,#199971,#199972,#199973,#199974,#199975,
#199976,#199977,#199978,#199979,#199980,#199981,#199982,#199983,#199984,
#199985,#199986,#199987,#199988,#199989,#199990,#199991,#199992,#199993,
#199994,#199995,#199996,#199997,#199998,#199999,#200000,#200001,#200002,
#200003,#200004,#200005,#200006,#200007,#200008,#200009,#200010,#200011,
#200012,#200013,#200014,#200015,#200016,#200017,#200018,#200019,#200020,
#200021,#200022,#200023),.UNSPECIFIED.,.F.,.F.,(4,2,2,2,2,2,2,2,2,2,2,2,
2,2,2,2,2,2,2,2,2,2,2,2,2,2,2,2,2,2,2,2,2,2,2,2,2,2,2,2,2,2,2,2,2,2,2,2,
2,2,2,2,2,2,2,2,2,2,2,2,2,2,2,2,2,2,2,2,2,2,2,2,2,2,2,2,2,2,2,2,2,2,2,2,
2,2,2,2,2,2,2,2,2,2,2,2,2,2,2,2,2,2,2,2,2,2,2,2,2,2,2,4),(0.0751024976388681,
0.100173146895298,0.113801182309511,0.129357242395927,0.154621270231427,
0.16574502811648,0.168013829907005,0.169270713533231,0.170341757364332,
0.171688227814516,0.174304768538712,0.190264821349283,0.195792699913727,
0.252782593681776,0.268941064366794,0.27273664188936,0.274930502925903,
0.276843613715273,0.279204068839098,0.282809998823665,0.299513718575246,
0.30701523152462,0.355518416127759,0.370247953838068,0.378141906569891,
0.380173618302696,0.381376818270048,0.382456614250652,0.383863547667469,
0.38622998851002,0.401654001311554,0.405922021285589,0.448897014545642,
0.476829270098281,0.483169635994594,0.485862175594031,0.487820654124135,
0.489616203486893,0.49249867592284,0.499491545958294,0.551012816803328,
0.578035821914904,0.589621346486818,0.591909302009542,0.593168926512293,
0.594239777664312,0.59558279881323,0.598183268064083,0.613748740242112,
0.620207314566039,0.661617986531234,0.688887761373014,0.695147609107977,
0.697826437144618,0.699782539677545,0.701581200064785,0.704480340061765,
0.711572868475071,0.761226455833534,0.799536600739436,0.803140683842643,
0.804654538342414,0.805747372631676,0.806771681940235,0.808507261882338,
0.813191793391958,0.854271180339101,0.900697354279703,0.907088807858633,
0.90979014053422,0.911750302102162,0.913544140542142,0.91641674981925,0.923349173805305,
0.975792202674048,1.00216420832525,1.01358792934847,1.01586689475685,1.01712462306176,
1.01819570758363,1.01954136601911,1.02215379793928,1.0380040447313,1.04274741961133,
1.05802455246317,1.09089766918535,1.10747811641254,1.11779738653335,1.12104689433375,
1.12312030072295,1.12506076024193,1.12760121510776,1.13189407062283,1.17429131127521,
1.20334665408896,1.2229611694138,1.22691606494033,1.22848762138044,1.22959112098465,
1.23060151308425,1.23226500850481,1.23648980762861,1.28582954827231,1.32659526345396,
1.33166117468821,1.33412063709304,1.33604348664034,1.33817496755308,1.34168746194444,
1.35456256393462,1.37726334489159,1.40841236097604),.UNSPECIFIED.);
#2027=B_SPLINE_CURVE_WITH_KNOTS('',3,(#200029,#200030,#200031,#200032),
 .UNSPECIFIED.,.F.,.F.,(4,4),(114.406674973168,114.756144668717),
 .UNSPECIFIED.);
#2028=B_SPLINE_CURVE_WITH_KNOTS('',3,(#200033,#200034,#200035,#200036,#200037,
#200038,#200039,#200040,#200041,#200042,#200043,#200044,#200045,#200046,
#200047,#200048,#200049,#200050,#200051,#200052,#200053,#200054,#200055,
#200056,#200057,#200058,#200059,#200060,#200061,#200062,#200063,#200064,
#200065,#200066,#200067,#200068,#200069,#200070,#200071,#200072,#200073,
#200074,#200075,#200076,#200077,#200078,#200079,#200080,#200081,#200082,
#200083,#200084,#200085,#200086,#200087,#200088,#200089,#200090,#200091,
#200092,#200093,#200094,#200095,#200096,#200097,#200098,#200099,#200100,
#200101,#200102,#200103,#200104,#200105,#200106,#200107,#200108,#200109,
#200110,#200111,#200112,#200113,#200114,#200115,#200116,#200117,#200118,
#200119,#200120,#200121,#200122,#200123,#200124,#200125,#200126,#200127,
#200128,#200129,#200130,#200131,#200132,#200133,#200134,#200135,#200136,
#200137,#200138,#200139,#200140,#200141,#200142,#200143,#200144,#200145,
#200146,#200147,#200148,#200149,#200150,#200151,#200152,#200153,#200154,
#200155,#200156,#200157,#200158,#200159,#200160,#200161,#200162,#200163,
#200164,#200165,#200166,#200167,#200168,#200169,#200170,#200171,#200172,
#200173,#200174,#200175,#200176,#200177,#200178,#200179,#200180,#200181,
#200182,#200183,#200184,#200185,#200186,#200187,#200188,#200189,#200190,
#200191,#200192,#200193,#200194,#200195,#200196,#200197,#200198,#200199,
#200200,#200201,#200202,#200203,#200204,#200205,#200206,#200207,#200208,
#200209,#200210,#200211,#200212,#200213,#200214,#200215,#200216,#200217,
#200218,#200219,#200220,#200221,#200222,#200223,#200224,#200225,#200226,
#200227,#200228,#200229,#200230,#200231,#200232,#200233,#200234,#200235,
#200236,#200237,#200238,#200239,#200240,#200241,#200242,#200243,#200244,
#200245,#200246,#200247,#200248,#200249,#200250,#200251,#200252),
 .UNSPECIFIED.,.F.,.F.,(4,2,2,2,2,2,2,2,2,2,2,2,2,2,2,2,2,2,2,2,2,2,2,2,
2,2,2,2,2,2,2,2,2,2,2,2,2,2,2,2,2,2,2,2,2,2,2,2,2,2,2,2,2,2,2,2,2,2,2,2,
2,2,2,2,2,2,2,2,2,2,2,2,2,2,2,2,2,2,2,2,2,2,2,2,2,2,2,2,2,2,2,2,2,2,2,2,
2,2,2,2,2,2,2,2,2,2,2,2,2,4),(0.000658788894674154,0.00332970132034127,
0.00592165829033243,0.00778879648581875,0.00964368923404936,0.0114909184853086,
0.0146445377053462,0.0233614970618546,0.092229541711162,0.109144084551986,
0.112803141256342,0.114326472957728,0.115421149470292,0.116443232178583,
0.118166704238405,0.122770276101425,0.165872185719283,0.208362522370533,
0.213664594158701,0.216707561179275,0.218819371417798,0.220855490232865,
0.222735969728323,0.225227342514191,0.229351510339336,0.256647990146848,
0.299685109788396,0.315418438681117,0.323672694298771,0.32573518356848,
0.326945458119776,0.328023929938131,0.329419151128872,0.331744783434459,
0.346117811018334,0.35471782018955,0.367795135811537,0.400650498847912,
0.417205081784512,0.427513198543129,0.430761824601561,0.432835300478543,
0.434776269046985,0.437318030994917,0.441614531091708,0.476730751585137,
0.525632470784906,0.535444939306928,0.53762421666097,0.538860394860561,
0.539934225817554,0.541310786866089,0.544162526319072,0.580485084603969,
0.63432567418599,0.640783781255109,0.643496853714483,0.645459583395521,
0.647251682948482,0.650112617667215,0.65697091859575,0.710435266942078,
0.736113857521736,0.747362715689847,0.749632144645471,0.750888030278971,
0.751959623668511,0.753308568550604,0.755935169058406,0.772041733613367,
0.77251762365382,0.823030705846806,0.840706703734584,0.851514906899761,
0.854819828013481,0.856905747406168,0.858842114811428,0.861354716666702,
0.865550838001097,0.895444937635017,0.94730779998003,0.959334192030385,
0.961646875854829,0.962912173502525,0.963983109465477,0.965320260546943,
0.967403656729176,0.977474780762184,0.982987097800833,0.99237762543089,
1.00394871724414,1.03679626470523,1.05333776343544,1.06364040669498,1.06688873198901,
1.06896235837823,1.07090370849627,1.07344631743539,1.07774502806268,1.11305593701797,
1.16231140812583,1.1716492636795,1.17379556394198,1.17502460294623,1.17609973025966,
1.17748782717431,1.18039792620084,1.20852959895016,1.24821969646968,1.26019912898447),
 .UNSPECIFIED.);
#2029=B_SPLINE_CURVE_WITH_KNOTS('',3,(#200254,#200255,#200256,#200257,#200258,
#200259,#200260,#200261,#200262,#200263,#200264,#200265,#200266,#200267,
#200268,#200269,#200270,#200271,#200272,#200273,#200274,#200275,#200276,
#200277,#200278,#200279,#200280,#200281,#200282,#200283,#200284,#200285,
#200286,#200287,#200288,#200289,#200290,#200291,#200292,#200293,#200294,
#200295,#200296,#200297,#200298,#200299,#200300,#200301,#200302,#200303,
#200304,#200305,#200306,#200307,#200308,#200309,#200310,#200311,#200312,
#200313,#200314,#200315,#200316,#200317,#200318,#200319,#200320,#200321,
#200322,#200323,#200324,#200325,#200326,#200327,#200328,#200329,#200330,
#200331,#200332,#200333,#200334,#200335,#200336,#200337,#200338,#200339,
#200340,#200341,#200342,#200343,#200344,#200345,#200346,#200347,#200348,
#200349,#200350,#200351,#200352,#200353,#200354,#200355,#200356,#200357,
#200358,#200359,#200360,#200361,#200362,#200363,#200364,#200365,#200366,
#200367,#200368,#200369,#200370,#200371,#200372,#200373,#200374,#200375,
#200376,#200377,#200378,#200379,#200380,#200381,#200382,#200383,#200384,
#200385,#200386,#200387,#200388,#200389,#200390,#200391,#200392,#200393,
#200394,#200395,#200396,#200397,#200398,#200399,#200400,#200401,#200402,
#200403,#200404,#200405,#200406,#200407,#200408,#200409,#200410,#200411,
#200412,#200413,#200414,#200415,#200416,#200417,#200418,#200419,#200420,
#200421,#200422,#200423,#200424,#200425,#200426,#200427,#200428,#200429,
#200430,#200431,#200432,#200433,#200434,#200435,#200436,#200437,#200438,
#200439,#200440,#200441,#200442,#200443,#200444,#200445,#200446,#200447,
#200448,#200449,#200450,#200451,#200452,#200453,#200454,#200455,#200456,
#200457,#200458,#200459,#200460,#200461,#200462,#200463,#200464,#200465,
#200466,#200467,#200468,#200469,#200470,#200471),.UNSPECIFIED.,.F.,.F.,
(4,2,2,2,2,2,2,2,2,2,2,2,2,2,2,2,2,2,2,2,2,2,2,2,2,2,2,2,2,2,2,2,2,2,2,
2,2,2,2,2,2,2,2,2,2,2,2,2,2,2,2,2,2,2,2,2,2,2,2,2,2,2,2,2,2,2,2,2,2,2,2,
2,2,2,2,2,2,2,2,2,2,2,2,2,2,2,2,2,2,2,2,2,2,2,2,2,2,2,2,2,2,2,2,2,2,2,2,
2,4),(1.40841236097604,1.41585081406069,1.42084495972905,1.43685104509067,
1.43947024757663,1.44081735202331,1.44188851260067,1.44314508967006,1.445418801523,
1.45675138344984,1.48276078399497,1.53567732968201,1.54257225267126,1.54543866432514,
1.54723135854491,1.54919246489714,1.55189911235796,1.55832207571103,1.58694450706505,
1.63822367807732,1.64928437009302,1.65143120163553,1.65278753024501,1.65385936201447,
1.65510905838423,1.6573510722311,1.66814613729271,1.69210614285944,1.74805427396802,
1.75467945962303,1.7572186345253,1.759044417037,1.76098286815877,1.76355580451578,
1.76921984354574,1.79186040852704,1.82467554360162,1.82894784270214,1.8603909912648,
1.86330242500633,1.8646903486468,1.86576496494066,1.86699300744002,1.86913658671504,
1.87844771779498,1.92759189116734,1.96295389057885,1.96725105524298,1.96979258787608,
1.9717330120747,1.97380554763751,1.97705195047991,1.98734661357816,2.00387581172515,
2.03673162265381,2.04840005046803,2.0570704174793,2.07274531215951,2.07535037524001,
2.07669433642549,2.07776517879802,2.07902391684396,2.08130800879691,2.0928269691322,
2.11958001108092,2.17143120860544,2.17839959343032,2.18127790274253,2.18307261111663,
2.1850315782303,2.18772734339576,2.19408722180299,2.25006525654493,2.27220693590807,
2.28496370072602,2.28720592872981,2.28859105841952,2.28966533389733,2.29089502958668,
2.29304629673985,2.30246579198581,2.35165424156335,2.38684772922228,2.39114259589775,
2.39368338998927,2.39562360765204,2.39769626899719,2.40094359186727,2.41104270525211,
2.42722893507529,2.46891343386274,2.49623218564847,2.49913555813965,2.50052184689885,
2.50159621630899,2.50282511775341,2.50411851950549,2.50878390124864,2.53289345834914,
2.55378951587328,2.59882588228687,2.60308236521915,2.60561202494915,2.60755044214656,
2.6096277104179,2.61289596265875,2.61669868245321,2.62396228455341,2.66758385820486),
 .UNSPECIFIED.);
#2030=B_SPLINE_CURVE_WITH_KNOTS('',3,(#200472,#200473,#200474,#200475,#200476,
#200477,#200478,#200479,#200480,#200481,#200482,#200483,#200484,#200485,
#200486,#200487,#200488,#200489,#200490,#200491),.UNSPECIFIED.,.F.,.F.,
(4,2,2,2,2,2,2,2,2,4),(0.000649992924200273,0.037515273389423,0.0412926063506684,
0.0433020337866211,0.0446072154259599,0.0458444190226681,0.0469177316247823,
0.0482917908521054,0.0511320595409267,0.0747588858459464),.UNSPECIFIED.);
#2031=B_SPLINE_CURVE_WITH_KNOTS('',3,(#200497,#200498,#200499,#200500,#200501,
#200502,#200503,#200504,#200505,#200506),.UNSPECIFIED.,.F.,.F.,(4,3,3,4),
(120.689857252469,120.859210445387,120.962579625184,121.040543977909),
 .UNSPECIFIED.);
#2032=B_SPLINE_CURVE_WITH_KNOTS('',3,(#200507,#200508,#200509,#200510,#200511,
#200512,#200513,#200514,#200515,#200516),.UNSPECIFIED.,.F.,.F.,(4,1,1,1,
1,1,1,4),(114.756144668717,114.866191745616,115.865028195577,116.863864645539,
117.862701095501,118.861537545463,119.860373995425,120.689851223097),
 .UNSPECIFIED.);
#2033=B_SPLINE_CURVE_WITH_KNOTS('',3,(#200517,#200518,#200519,#200520,#200521,
#200522,#200523,#200524,#200525,#200526,#200527,#200528,#200529,#200530,
#200531,#200532,#200533,#200534,#200535,#200536,#200537,#200538,#200539,
#200540,#200541,#200542,#200543,#200544,#200545,#200546,#200547,#200548,
#200549,#200550,#200551,#200552,#200553,#200554,#200555,#200556,#200557,
#200558,#200559,#200560,#200561,#200562,#200563,#200564,#200565,#200566,
#200567,#200568,#200569,#200570,#200571,#200572,#200573,#200574,#200575,
#200576,#200577,#200578,#200579,#200580,#200581,#200582,#200583,#200584,
#200585,#200586,#200587,#200588,#200589,#200590,#200591,#200592,#200593,
#200594,#200595,#200596,#200597,#200598,#200599,#200600,#200601,#200602,
#200603,#200604,#200605,#200606,#200607,#200608,#200609,#200610,#200611,
#200612,#200613,#200614,#200615,#200616,#200617,#200618,#200619,#200620,
#200621,#200622,#200623,#200624,#200625,#200626,#200627,#200628,#200629,
#200630,#200631,#200632,#200633,#200634,#200635,#200636,#200637,#200638,
#200639,#200640,#200641,#200642,#200643,#200644,#200645,#200646,#200647,
#200648,#200649,#200650,#200651,#200652,#200653,#200654,#200655,#200656,
#200657,#200658,#200659,#200660,#200661,#200662,#200663,#200664,#200665,
#200666,#200667,#200668,#200669,#200670,#200671,#200672,#200673,#200674,
#200675,#200676,#200677,#200678,#200679,#200680,#200681,#200682,#200683,
#200684,#200685,#200686,#200687,#200688,#200689,#200690,#200691,#200692,
#200693,#200694,#200695,#200696,#200697,#200698,#200699,#200700,#200701,
#200702,#200703,#200704,#200705,#200706,#200707,#200708,#200709,#200710,
#200711,#200712,#200713,#200714,#200715,#200716,#200717,#200718,#200719,
#200720,#200721,#200722,#200723,#200724,#200725,#200726,#200727,#200728,
#200729,#200730,#200731,#200732,#200733,#200734),.UNSPECIFIED.,.F.,.F.,
(4,2,2,2,2,2,2,2,2,2,2,2,2,2,2,2,2,2,2,2,2,2,2,2,2,2,2,2,2,2,2,2,2,2,2,
2,2,2,2,2,2,2,2,2,2,2,2,2,2,2,2,2,2,2,2,2,2,2,2,2,2,2,2,2,2,2,2,2,2,2,2,
2,2,2,2,2,2,2,2,2,2,2,2,2,2,2,2,2,2,2,2,2,2,2,2,2,2,2,2,2,2,2,2,2,2,2,2,
2,4),(0.0747588858459464,0.0879797100071701,0.109399210605851,0.1361824288672,
0.146436093238305,0.149706957161066,0.151785046590808,0.1537236459466,0.156252708008424,
0.160506359700356,0.193188587404338,0.222560667390916,0.244175416228302,
0.254295391077272,0.256485297263878,0.25773343018092,0.258805433744377,
0.260163916946221,0.262836074139897,0.280219844032183,0.329263015910941,
0.34730554909262,0.3545735683608,0.360002510934368,0.362567737056095,0.364505076273853,
0.366333274476484,0.368881377847341,0.375563261598372,0.430967218228503,
0.45531854455265,0.466218383893618,0.468466837905448,0.469717974758843,
0.470789723056959,0.472144248604246,0.474885982334562,0.493328942238641,
0.537460382854009,0.565331826300443,0.57166532396708,0.574356959584286,
0.576315520801497,0.578111658932356,0.580996202893888,0.587999848161857,
0.639384588344836,0.666515502702058,0.678128415070438,0.680418167992362,
0.681678308392531,0.682749313041741,0.684092165345215,0.68669125548634,
0.702216899000038,0.708760971634423,0.72263387812871,0.755493941726029,
0.772056444543111,0.782367868914643,0.785616673179452,0.787690055163526,
0.789630789989735,0.792172035406727,0.796467190705044,0.831578304350796,
0.880465439404303,0.890288614785536,0.892468472230853,0.893704703836293,
0.894778405091688,0.896154569949096,0.899004699646103,0.93537456298567,
0.989163016853752,0.99561907129515,0.998331639332602,1.00029413354789,1.00208610698246,
1.00494703321247,1.01180631146846,1.06524491881451,1.09093516386653,1.10218656064975,
1.10445597823434,1.10571178682071,1.10678327142763,1.10813202452887,1.11075808991063,
1.12692228326169,1.17758027648585,1.20199424684519,1.20789426565626,1.21051032975775,
1.21245602804851,1.21427042462654,1.21676503388208,1.2231148806821,1.28150383668905,
1.3039545071262,1.31433172996214,1.31654813469475,1.31779242056303,1.31886514467892,
1.32022973899236,1.32240314909759,1.3338998499708,1.38263544072133,1.40832418655118),
 .UNSPECIFIED.);
#2034=B_SPLINE_CURVE_WITH_KNOTS('',3,(#200740,#200741,#200742,#200743,#200744,
#200745,#200746,#200747),.UNSPECIFIED.,.F.,.F.,(4,2,2,4),(2.5938719493606,
2.59862224991634,2.62666588587967,2.66835909139805),.UNSPECIFIED.);
#2035=B_SPLINE_CURVE_WITH_KNOTS('',3,(#200748,#200749,#200750,#200751,#200752,
#200753,#200754,#200755,#200756,#200757,#200758,#200759,#200760,#200761,
#200762,#200763,#200764,#200765,#200766,#200767,#200768,#200769,#200770,
#200771,#200772,#200773,#200774,#200775,#200776,#200777,#200778,#200779,
#200780,#200781,#200782,#200783,#200784,#200785,#200786,#200787,#200788,
#200789,#200790,#200791,#200792,#200793,#200794,#200795,#200796,#200797,
#200798,#200799,#200800,#200801,#200802,#200803,#200804,#200805,#200806,
#200807,#200808,#200809,#200810,#200811,#200812,#200813,#200814,#200815,
#200816,#200817,#200818,#200819,#200820,#200821,#200822,#200823,#200824,
#200825,#200826,#200827,#200828,#200829,#200830,#200831,#200832,#200833,
#200834,#200835,#200836,#200837,#200838,#200839,#200840,#200841,#200842,
#200843,#200844,#200845,#200846,#200847,#200848,#200849,#200850,#200851,
#200852,#200853,#200854,#200855,#200856,#200857,#200858,#200859,#200860,
#200861,#200862,#200863,#200864,#200865,#200866,#200867,#200868,#200869,
#200870,#200871,#200872,#200873,#200874,#200875,#200876,#200877,#200878,
#200879,#200880,#200881,#200882,#200883,#200884,#200885,#200886,#200887,
#200888,#200889,#200890,#200891,#200892,#200893,#200894,#200895,#200896,
#200897,#200898,#200899,#200900,#200901,#200902,#200903,#200904,#200905,
#200906,#200907,#200908,#200909,#200910,#200911,#200912,#200913,#200914,
#200915,#200916,#200917,#200918,#200919,#200920,#200921,#200922,#200923,
#200924,#200925),.UNSPECIFIED.,.F.,.F.,(4,3,3,3,3,3,3,3,3,3,3,3,3,3,3,3,
3,3,3,3,3,3,3,3,3,3,3,3,3,3,3,3,3,3,3,3,3,3,3,3,3,3,3,3,3,3,3,3,3,3,3,3,
3,3,3,3,3,3,3,4),(121.040543977909,121.143685186123,121.246752639545,121.34978039127,
121.452802442928,121.555926066816,121.659098529552,121.762462041336,121.858046895349,
121.961441632397,122.064682914512,122.167802879905,122.270857448114,122.373880656471,
122.476906499144,122.580039265922,122.683228357332,122.786600350714,122.856883345311,
122.960278082359,123.063519364473,123.166639329866,123.269693898074,123.372717106432,
123.475742949104,123.578875715882,123.682064807291,123.785436800673,123.855719795272,
123.95911453232,124.062355814435,124.165475779827,124.268530348036,124.371553556394,
124.474579399066,124.577712165844,124.680901257254,124.784273250636,124.854556245234,
124.957950982282,125.061192264397,125.16431222979,125.267366797999,125.370390006357,
125.473415849029,125.576548615808,125.679737707218,125.783109700599,125.853392695196,
125.956787432244,126.060028714359,126.163148679751,126.26620324796,126.369226456318,
126.472252298991,126.575385065769,126.678574157179,126.78194615056,126.852229145158,
126.973042559648),.UNSPECIFIED.);
#2036=B_SPLINE_CURVE_WITH_KNOTS('',3,(#200927,#200928,#200929,#200930,#200931,
#200932,#200933,#200934,#200935,#200936,#200937,#200938,#200939,#200940,
#200941,#200942,#200943,#200944,#200945,#200946,#200947,#200948,#200949,
#200950,#200951,#200952,#200953,#200954,#200955,#200956,#200957,#200958,
#200959,#200960,#200961,#200962,#200963,#200964,#200965,#200966,#200967,
#200968,#200969,#200970,#200971,#200972,#200973,#200974,#200975,#200976,
#200977,#200978,#200979,#200980,#200981,#200982,#200983,#200984,#200985,
#200986,#200987,#200988,#200989,#200990,#200991,#200992,#200993,#200994,
#200995,#200996,#200997,#200998,#200999,#201000,#201001,#201002,#201003,
#201004,#201005,#201006,#201007,#201008,#201009,#201010,#201011,#201012,
#201013,#201014,#201015,#201016,#201017,#201018,#201019,#201020,#201021,
#201022,#201023,#201024,#201025,#201026,#201027,#201028,#201029,#201030,
#201031,#201032,#201033,#201034,#201035,#201036,#201037,#201038,#201039,
#201040,#201041,#201042,#201043,#201044,#201045,#201046,#201047,#201048,
#201049,#201050,#201051,#201052,#201053,#201054,#201055,#201056,#201057,
#201058,#201059,#201060,#201061,#201062,#201063,#201064,#201065,#201066,
#201067,#201068,#201069,#201070,#201071,#201072,#201073,#201074,#201075,
#201076,#201077,#201078,#201079,#201080,#201081,#201082,#201083,#201084,
#201085,#201086,#201087,#201088,#201089,#201090,#201091,#201092,#201093,
#201094,#201095,#201096,#201097,#201098,#201099,#201100,#201101,#201102,
#201103,#201104,#201105,#201106,#201107,#201108,#201109,#201110,#201111,
#201112,#201113,#201114,#201115,#201116,#201117,#201118,#201119,#201120,
#201121,#201122,#201123,#201124,#201125,#201126,#201127,#201128,#201129,
#201130,#201131,#201132,#201133,#201134,#201135,#201136,#201137,#201138,
#201139,#201140,#201141,#201142,#201143,#201144,#201145,#201146,#201147,
#201148,#201149,#201150,#201151,#201152,#201153,#201154,#201155,#201156,
#201157,#201158,#201159,#201160,#201161,#201162,#201163,#201164,#201165,
#201166,#201167,#201168,#201169,#201170,#201171,#201172,#201173,#201174,
#201175,#201176,#201177,#201178,#201179,#201180,#201181,#201182,#201183,
#201184,#201185,#201186,#201187,#201188,#201189,#201190),.UNSPECIFIED.,
 .F.,.F.,(4,2,2,2,2,2,2,2,2,2,2,2,2,2,2,2,2,2,2,2,2,2,2,2,2,2,2,2,2,2,2,
2,2,2,2,2,2,2,2,2,2,2,2,2,2,2,2,2,2,2,2,2,2,2,2,2,2,2,2,2,2,2,2,2,2,2,2,
2,2,2,2,2,2,2,2,2,2,2,2,2,2,2,2,2,2,2,2,2,2,2,2,2,2,2,2,2,2,2,2,2,2,2,2,
2,2,2,2,2,2,2,2,2,2,2,2,2,2,2,2,2,2,2,2,2,2,2,2,2,2,2,2,4),(1.40832418655118,
1.41583872157815,1.42010257572939,1.4226348669936,1.42457428742719,1.42665164267686,
1.42991795340268,1.44038101522293,1.4572819688539,1.49511046458649,1.52518585406619,
1.52810044555585,1.5294892222838,1.53056419895257,1.53179231764653,1.53393524396405,
1.54323139990793,1.56207794175142,1.60247841650693,1.61474051057434,1.62934634609348,
1.63313462366128,1.63534961323343,1.63726187255969,1.63959690251243,1.64404682602657,
1.67495957322253,1.72180664623564,1.73760389838481,1.7402163798589,1.74156226399387,
1.74263363332685,1.74389182374998,1.74617194177872,1.75760855961769,1.78402411855815,
1.83638765294265,1.8433261011902,1.84620018155187,1.8479946416121,1.849955250322,
1.85265676724047,1.85904660892856,1.88738479009089,1.93728384336638,1.94991437905467,
1.9521506667732,1.95353430165758,1.95460881103608,1.95584033888736,1.95799850500166,
1.96750669461709,2.01664172526128,2.05182798614575,2.05612434747821,2.05866610990359,
2.06060711544705,2.06268066541234,2.06592947855171,2.0762387027851,2.09279785893303,
2.12568540440676,2.13955073775261,2.14611503786987,2.16166396020909,2.16426434365899,
2.16560757339552,2.16667872461248,2.16793886303792,2.17022815481917,2.18182958993675,
2.20890891976209,2.26033584398661,2.26733480309933,2.2702187914972,2.27201499178972,
2.27397395214511,2.2766667313089,2.28300567537386,2.31092263620224,2.35691900429129,
2.3582212446484,2.37368714132845,2.3760558649217,2.37746369558322,2.37854390485505,
2.37974727321361,2.38177861880869,2.38966330880926,2.40436315051192,2.44559174097471,
2.47594830264476,2.48016553672262,2.48268423140849,2.48462145646318,2.48469685162256,
2.48474248809897,2.48478674315558,2.48482687148383,2.48486331755192,2.48489646882688,
2.48492666434582,2.48495420342987,2.48497934912401,2.48500233407452,2.48502336466585,
2.48504262448749,2.48506027729796,2.48507646954186,2.48509922830073,2.4851215630853,
2.48514348550655,2.48516501052931,2.4851861509435,2.48520691907636,2.48522732673606,
2.48524738528785,2.48750364533091,2.49161544699482,2.4967486418115,2.50777948381343,
2.53230080123694,2.54783910363152,2.58533079090176,2.58816258109248,2.58953513216007,
2.59060849255101,2.59184714882272,2.59403805432889,2.60402580906601,2.65274977226297,
2.6674812874869),.UNSPECIFIED.);
#2037=B_SPLINE_CURVE_WITH_KNOTS('',3,(#201191,#201192,#201193,#201194,#201195,
#201196,#201197,#201198,#201199,#201200,#201201,#201202,#201203,#201204,
#201205,#201206,#201207,#201208,#201209,#201210,#201211,#201212),
 .UNSPECIFIED.,.F.,.F.,(4,2,2,2,2,2,2,2,2,2,4),(0.000768638562662975,0.0217328432260458,
0.0248352869314532,0.0269713212508239,0.0287705216612541,0.0306857495874429,
0.0330701219975814,0.0367527850347077,0.0546136258233204,0.0730984127855758,
0.0751664351648031),.UNSPECIFIED.);
#2038=B_SPLINE_CURVE_WITH_KNOTS('',3,(#201217,#201218,#201219,#201220,#201221,
#201222,#201223,#201224,#201225,#201226,#201227,#201228,#201229,#201230,
#201231,#201232,#201233,#201234,#201235,#201236,#201237,#201238,#201239,
#201240,#201241,#201242,#201243,#201244,#201245,#201246,#201247,#201248,
#201249,#201250,#201251,#201252,#201253,#201254,#201255,#201256,#201257,
#201258,#201259,#201260,#201261,#201262,#201263,#201264,#201265,#201266,
#201267,#201268,#201269,#201270,#201271,#201272,#201273,#201274,#201275,
#201276,#201277,#201278,#201279,#201280,#201281,#201282,#201283,#201284,
#201285,#201286,#201287,#201288,#201289,#201290,#201291,#201292,#201293,
#201294,#201295,#201296,#201297,#201298,#201299,#201300,#201301,#201302,
#201303,#201304,#201305,#201306,#201307,#201308,#201309,#201310,#201311,
#201312,#201313,#201314,#201315,#201316,#201317,#201318,#201319,#201320,
#201321,#201322,#201323,#201324,#201325,#201326,#201327,#201328,#201329,
#201330,#201331,#201332,#201333,#201334,#201335,#201336,#201337,#201338,
#201339,#201340,#201341,#201342,#201343,#201344,#201345,#201346,#201347,
#201348,#201349,#201350,#201351,#201352,#201353,#201354,#201355,#201356,
#201357,#201358,#201359,#201360,#201361,#201362,#201363,#201364,#201365,
#201366,#201367,#201368,#201369,#201370,#201371,#201372,#201373,#201374,
#201375,#201376,#201377,#201378,#201379,#201380,#201381,#201382,#201383,
#201384,#201385,#201386,#201387,#201388,#201389,#201390,#201391,#201392,
#201393,#201394,#201395,#201396,#201397,#201398,#201399,#201400,#201401,
#201402,#201403,#201404,#201405,#201406,#201407,#201408,#201409,#201410,
#201411,#201412,#201413,#201414,#201415,#201416,#201417,#201418,#201419,
#201420,#201421,#201422,#201423,#201424,#201425,#201426,#201427,#201428,
#201429,#201430,#201431,#201432,#201433,#201434,#201435,#201436,#201437,
#201438,#201439,#201440,#201441,#201442,#201443,#201444,#201445,#201446,
#201447,#201448,#201449,#201450,#201451,#201452),.UNSPECIFIED.,.F.,.F.,
(4,2,2,2,2,2,2,2,2,2,2,2,2,2,2,2,2,2,2,2,2,2,2,2,2,2,2,2,2,2,2,2,2,2,2,
2,2,2,2,2,2,2,2,2,2,2,2,2,2,2,2,2,2,2,2,2,2,2,2,2,2,2,2,2,2,2,2,2,2,2,2,
2,2,2,2,2,2,2,2,2,2,2,2,2,2,2,2,2,2,2,2,2,2,2,2,2,2,2,2,2,2,2,2,2,2,2,2,
2,2,2,2,2,2,2,2,2,2,4),(1.25996976443291,1.27817361085212,1.30767742298493,
1.31208784385346,1.31441477689738,1.3161418694476,1.31829830389366,1.32192113954004,
1.33437189970869,1.38533272483373,1.41654250559185,1.4194556905084,1.42084434731202,
1.4219194844673,1.42314806984404,1.42529247407934,1.43460529192529,1.48376433305904,
1.51915472469176,1.52345408005697,1.52599686704145,1.52793822513192,1.53001173511723,
1.53325961618488,1.54355856207559,1.56009425210006,1.59296459462998,1.60449112209311,
1.61424405337767,1.61613067747189,1.62921218400807,1.63147177164606,1.63286244468406,
1.63393772572315,1.63516489280432,1.63730312334334,1.64653235436676,1.66516775824721,
1.70928295141884,1.73178833335573,1.73573347955207,1.73819841855544,1.74012247611274,
1.74225215532024,1.74575445084859,1.75851110058937,1.78090243119528,1.82131909217728,
1.82560552285894,1.82817328265896,1.84121561111651,1.84347319952846,1.84486326513884,
1.84593847223012,1.84716599696492,1.84930588295451,1.85855805352352,1.87726537301691,
1.9214776507342,1.94380175410119,1.9477390887044,1.95020165156345,1.95212540689174,
1.95425633864387,1.95776434765773,1.97058270806592,1.99313317729192,2.0445576670405,
2.05370287779019,2.05591496086657,2.05717173628615,2.05824336245306,2.0595914236533,
2.06229969955907,2.08724550384447,2.13283196920506,2.15579518609972,2.15976036328525,
2.16223142123502,2.1641563080508,2.16628288744377,2.16977088182105,2.18237378370215,
2.23320115794848,2.26466186980415,2.26756932863816,2.26895689154742,2.2700319360336,
2.27126125988575,2.27340893395648,2.28276669661786,2.33204117454941,2.36727110126,
2.37156857205427,2.37411084201532,2.37605214943738,2.37812593881716,2.38137495363604,
2.39168335653041,2.40823980370276,2.47089936102958,2.47226100486589,2.47844116564448,
2.48038049069598,2.48156360485752,2.48259548735953,2.48400849450304,2.48702260108564,
2.49111903976041,2.50139060443183,2.52422264305586,2.57594785564152,2.58293221503037,
2.58581439829049,2.58761071994399,2.58957080718724,2.5922669462497,2.5938719493606),
 .UNSPECIFIED.);
#2039=B_SPLINE_CURVE_WITH_KNOTS('',3,(#201453,#201454,#201455,#201456,#201457,
#201458,#201459,#201460,#201461,#201462,#201463,#201464,#201465,#201466,
#201467,#201468,#201469,#201470,#201471,#201472,#201473,#201474,#201475,
#201476,#201477,#201478,#201479,#201480,#201481,#201482,#201483,#201484,
#201485,#201486,#201487,#201488,#201489,#201490,#201491,#201492,#201493,
#201494,#201495,#201496,#201497,#201498,#201499,#201500,#201501,#201502,
#201503,#201504,#201505,#201506,#201507,#201508,#201509,#201510,#201511,
#201512,#201513,#201514,#201515,#201516,#201517,#201518,#201519,#201520,
#201521,#201522,#201523,#201524,#201525,#201526,#201527,#201528,#201529,
#201530,#201531,#201532,#201533,#201534,#201535,#201536,#201537,#201538,
#201539,#201540,#201541,#201542,#201543,#201544,#201545,#201546,#201547,
#201548,#201549,#201550,#201551,#201552,#201553,#201554,#201555,#201556,
#201557,#201558,#201559,#201560,#201561,#201562,#201563,#201564,#201565,
#201566,#201567,#201568,#201569,#201570,#201571,#201572,#201573,#201574,
#201575,#201576,#201577,#201578,#201579,#201580,#201581,#201582,#201583,
#201584,#201585,#201586,#201587,#201588,#201589,#201590,#201591,#201592,
#201593,#201594,#201595,#201596,#201597,#201598,#201599,#201600,#201601,
#201602,#201603,#201604,#201605,#201606,#201607,#201608,#201609,#201610,
#201611,#201612,#201613,#201614,#201615,#201616,#201617,#201618,#201619,
#201620,#201621,#201622,#201623,#201624,#201625,#201626,#201627,#201628,
#201629,#201630,#201631,#201632,#201633,#201634,#201635,#201636,#201637,
#201638,#201639,#201640,#201641,#201642,#201643,#201644,#201645,#201646,
#201647,#201648,#201649,#201650,#201651,#201652,#201653,#201654,#201655,
#201656,#201657,#201658,#201659,#201660,#201661,#201662,#201663,#201664,
#201665,#201666,#201667,#201668,#201669,#201670,#201671,#201672,#201673,
#201674,#201675,#201676,#201677,#201678,#201679,#201680,#201681,#201682,
#201683,#201684,#201685,#201686,#201687,#201688,#201689,#201690),
 .UNSPECIFIED.,.F.,.F.,(4,2,2,2,2,2,2,2,2,2,2,2,2,2,2,2,2,2,2,2,2,2,2,2,
2,2,2,2,2,2,2,2,2,2,2,2,2,2,2,2,2,2,2,2,2,2,2,2,2,2,2,2,2,2,2,2,2,2,2,2,
2,2,2,2,2,2,2,2,2,2,2,2,2,2,2,2,2,2,2,2,2,2,2,2,2,2,2,2,2,2,2,2,2,2,2,2,
2,2,2,2,2,2,2,2,2,2,2,2,2,2,2,2,2,2,2,2,2,2,4),(0.0751664351648031,0.122346988242776,
0.131739194028345,0.133888806838276,0.135118276127824,0.1361928262999,0.137578921985736,
0.139823906855139,0.152628924282625,0.175045242086882,0.176210251072167,
0.208995272148526,0.225468169851392,0.232290879392018,0.237477834907157,
0.239949624495637,0.241788408939016,0.24361212485394,0.246142773384682,
0.252712751909429,0.30921693134264,0.33285432384443,0.34356160478676,0.345798534369181,
0.347047242671779,0.34811937263827,0.349477543323348,0.35163003158643,0.362779252651479,
0.413985155630467,0.442564674332054,0.44898357179459,0.451689848675295,
0.453651177127508,0.455444416017757,0.458312430817586,0.465214979187494,
0.518090453251227,0.544171167015094,0.555522174530228,0.557797297791336,
0.559054333708411,0.560125694169351,0.561472800404662,0.564091274875453,
0.580077896377513,0.585051565819623,0.629888712394502,0.648403829159917,
0.659576321811341,0.662920461139756,0.665014916094884,0.666948150920659,
0.669441169827075,0.673570863440185,0.700887508256962,0.743165790636969,
0.759418905946359,0.767854581617672,0.769931853395434,0.771145420820618,
0.772223167090481,0.773612710819158,0.775918979638267,0.789956654166822,
0.791301275937858,0.798311946222876,0.811988063787585,0.844849725796133,
0.861411599515774,0.871723051859038,0.874972088233509,0.877045672001599,
0.878986633389305,0.881528229847167,0.885824100341373,0.920957123164556,
0.969904495249132,0.979663687783069,0.981839348924972,0.98307474229114,
0.984148702056385,0.985526487748217,0.988384407862714,1.01124436943733,
1.02401053854181,1.05686693545025,1.0734200073315,1.08372777741852,1.08697661061679,
1.08905029475539,1.09099151170807,1.09353367602977,1.09783102914395,1.13304642848679,
1.1822527497537,1.19171696001675,1.19387222900763,1.19510321528332,1.19617797727302,
1.19756288077777,1.19980305841912,1.2125046529123,1.23488278711341,1.26848763937002,
1.29386537302104,1.29813616405493,1.30043374327061,1.30232685311879,1.30456764276984,
1.30846688370272,1.32437589687919,1.33459835185838,1.37388350711125,1.40246828626482,
1.40538090048541,1.40676947902978,1.40784464482559,1.4087765566926),
 .UNSPECIFIED.);
#2040=B_SPLINE_CURVE_WITH_KNOTS('',3,(#201696,#201697,#201698,#201699,#201700,
#201701,#201702,#201703,#201704,#201705,#201706,#201707,#201708,#201709,
#201710,#201711,#201712,#201713,#201714,#201715),.UNSPECIFIED.,.F.,.F.,
(4,2,2,2,2,2,2,2,2,4),(2.59331776226468,2.59687882416504,2.60151583696546,
2.60324440012632,2.60426747560143,2.60536147889293,2.60688102367856,2.61051762964333,
2.62723443668624,2.66742808210211),.UNSPECIFIED.);
#2041=B_SPLINE_CURVE_WITH_KNOTS('',3,(#201716,#201717,#201718,#201719,#201720,
#201721,#201722,#201723,#201724,#201725,#201726,#201727,#201728,#201729,
#201730,#201731,#201732,#201733,#201734,#201735,#201736,#201737,#201738,
#201739,#201740,#201741,#201742,#201743,#201744,#201745,#201746,#201747,
#201748,#201749,#201750,#201751,#201752,#201753,#201754,#201755,#201756,
#201757,#201758,#201759,#201760,#201761,#201762,#201763,#201764,#201765,
#201766,#201767,#201768,#201769,#201770,#201771,#201772,#201773,#201774,
#201775,#201776,#201777,#201778,#201779,#201780,#201781,#201782,#201783,
#201784,#201785,#201786,#201787,#201788,#201789,#201790,#201791,#201792,
#201793,#201794,#201795,#201796,#201797,#201798,#201799,#201800,#201801,
#201802,#201803,#201804,#201805,#201806,#201807,#201808,#201809,#201810,
#201811,#201812,#201813,#201814,#201815,#201816,#201817,#201818,#201819,
#201820,#201821,#201822,#201823,#201824,#201825,#201826,#201827,#201828,
#201829,#201830,#201831,#201832,#201833,#201834,#201835,#201836,#201837,
#201838,#201839,#201840,#201841,#201842,#201843,#201844,#201845,#201846,
#201847,#201848,#201849,#201850,#201851,#201852,#201853,#201854,#201855,
#201856,#201857,#201858,#201859,#201860,#201861,#201862,#201863,#201864,
#201865,#201866,#201867,#201868,#201869,#201870,#201871,#201872,#201873,
#201874,#201875,#201876,#201877,#201878,#201879,#201880,#201881,#201882,
#201883,#201884,#201885,#201886,#201887,#201888,#201889,#201890,#201891,
#201892,#201893,#201894,#201895,#201896,#201897,#201898,#201899,#201900,
#201901,#201902,#201903,#201904,#201905,#201906,#201907,#201908,#201909,
#201910,#201911,#201912,#201913,#201914,#201915,#201916,#201917,#201918,
#201919,#201920,#201921,#201922,#201923,#201924,#201925,#201926,#201927,
#201928,#201929,#201930,#201931,#201932,#201933,#201934,#201935,#201936,
#201937,#201938,#201939,#201940,#201941,#201942,#201943),.UNSPECIFIED.,
 .F.,.F.,(4,2,2,2,2,2,2,2,2,2,2,2,2,2,2,2,2,2,2,2,2,2,2,2,2,2,2,2,2,2,2,
2,2,2,2,2,2,2,2,2,2,2,2,2,2,2,2,2,2,2,2,2,2,2,2,2,2,2,2,2,2,2,2,2,2,2,2,
2,2,2,2,2,2,2,2,2,2,2,2,2,2,2,2,2,2,2,2,2,2,2,2,2,2,2,2,2,2,2,2,2,2,2,2,
2,2,2,2,2,2,2,2,2,2,4),(0.000704176387045162,0.0257174322174643,0.0359847029828326,
0.0390634760632502,0.0411897927333798,0.0432709570732162,0.0452083127274846,
0.0477298836914721,0.0519579433509182,0.0833451108736209,0.108642544508692,
0.136441798274749,0.145889395539929,0.148042836964259,0.149273089934266,
0.150347412956808,0.151732015589897,0.153972226003156,0.166687678355829,
0.188909395211854,0.215758615574672,0.237101823061518,0.24525349541233,
0.251225010735527,0.253845482176166,0.255800832283127,0.257600841493377,
0.260506681045256,0.267638306195958,0.316560289453651,0.355576580857015,
0.359166447748164,0.360677966617491,0.361770469902082,0.362795547041832,
0.364534723615624,0.369242329256875,0.409907236760057,0.456724709819592,
0.463117778256212,0.465819532313761,0.46777990438124,0.469573869737443,
0.472446538760659,0.47937836588777,0.531836911889365,0.558204274393352,
0.569627264630605,0.571906337375766,0.573164158634075,0.574235342718159,
0.575581152168262,0.578193953237735,0.594051450236483,0.598845344651008,
0.614069728480908,0.646945161062718,0.663526294999738,0.673846133326886,
0.677095894888077,0.679169481159531,0.681110121641195,0.683650831617003,
0.687944158977412,0.7303396011891,0.759387452405715,0.774118491642773,0.782013616435622,
0.784045763351531,0.785249245910931,0.786329312856606,0.78773662210919,
0.790103743863349,0.805534003367715,0.812264938970139,0.826056928548069,
0.858917448528633,0.875479587581388,0.885790959134291,0.889039839149378,
0.891113291674948,0.893054108121677,0.895595482909654,0.899890907285595,
0.935010850491094,0.983922413167823,0.993719231293955,0.995897355068234,
0.997133235743125,0.99820703638444,0.999583856581085,1.00243715643119,1.0251180204931,
1.03806278363758,1.07091848092184,1.08747235741845,1.09778029013521,1.10102899440095,
1.1031025529331,1.10504362187498,1.10758554845504,1.11188240124442,1.14708029997422,
1.19623277295707,1.20575435496611,1.2079135712673,1.20914537292454,1.21021991596308,
1.21160331437633,1.21383866255834,1.22645024787071,1.23297812007256,1.23811063457995,
1.25996976443291),.UNSPECIFIED.);
#2042=B_SPLINE_CURVE_WITH_KNOTS('',3,(#201945,#201946,#201947,#201948,#201949,
#201950,#201951,#201952,#201953,#201954,#201955,#201956,#201957,#201958,
#201959,#201960,#201961,#201962,#201963,#201964,#201965,#201966,#201967,
#201968,#201969,#201970,#201971,#201972,#201973,#201974,#201975,#201976,
#201977,#201978,#201979,#201980,#201981,#201982,#201983,#201984,#201985,
#201986,#201987,#201988,#201989,#201990,#201991,#201992,#201993,#201994,
#201995,#201996,#201997,#201998,#201999,#202000,#202001,#202002,#202003,
#202004,#202005,#202006,#202007,#202008,#202009,#202010,#202011,#202012,
#202013,#202014,#202015,#202016,#202017,#202018,#202019,#202020,#202021,
#202022,#202023,#202024,#202025,#202026,#202027,#202028,#202029,#202030,
#202031,#202032,#202033,#202034,#202035,#202036,#202037,#202038,#202039,
#202040,#202041,#202042,#202043,#202044,#202045,#202046,#202047,#202048,
#202049,#202050,#202051,#202052,#202053,#202054,#202055,#202056,#202057,
#202058,#202059,#202060,#202061,#202062,#202063,#202064,#202065,#202066,
#202067,#202068,#202069,#202070,#202071,#202072,#202073,#202074,#202075,
#202076,#202077,#202078,#202079,#202080,#202081,#202082,#202083,#202084,
#202085,#202086,#202087,#202088,#202089,#202090,#202091,#202092,#202093,
#202094,#202095,#202096,#202097,#202098,#202099,#202100,#202101,#202102,
#202103,#202104,#202105,#202106,#202107,#202108,#202109,#202110,#202111,
#202112,#202113,#202114,#202115,#202116,#202117,#202118,#202119,#202120,
#202121,#202122,#202123,#202124,#202125,#202126,#202127,#202128,#202129,
#202130,#202131,#202132,#202133,#202134,#202135,#202136,#202137,#202138,
#202139,#202140,#202141,#202142,#202143,#202144,#202145,#202146,#202147,
#202148,#202149,#202150,#202151,#202152,#202153,#202154,#202155,#202156,
#202157,#202158,#202159,#202160,#202161,#202162,#202163,#202164,#202165,
#202166,#202167,#202168,#202169,#202170,#202171,#202172,#202173,#202174,
#202175,#202176,#202177,#202178,#202179,#202180,#202181,#202182,#202183,
#202184,#202185,#202186,#202187,#202188,#202189,#202190,#202191,#202192,
#202193,#202194,#202195,#202196),.UNSPECIFIED.,.F.,.F.,(4,2,2,2,2,2,2,2,
2,2,2,2,2,2,2,2,2,2,2,2,2,2,2,2,2,2,2,2,2,2,2,2,2,2,2,2,2,2,2,2,2,2,2,2,
2,2,2,2,2,2,2,2,2,2,2,2,2,2,2,2,2,2,2,2,2,2,2,2,2,2,2,2,2,2,2,2,2,2,2,2,
2,2,2,2,2,2,2,2,2,2,2,2,2,2,2,2,2,2,2,2,2,2,2,2,2,2,2,2,2,2,2,2,2,2,2,2,
2,2,2,2,2,2,2,2,2,4),(1.4087765566926,1.40907336275232,1.4112182322391,
1.42053668861001,1.46971412927234,1.50508398887219,1.50938325226647,1.51192606388548,
1.51386748627527,1.51594110902301,1.51918925871308,1.5294898306286,1.54602886699855,
1.57357620420324,1.58971959996764,1.600802714468,1.6150361174334,1.61735264301978,
1.61874531396276,1.61982360776035,1.62103570079976,1.62310576441306,1.6314496999546,
1.64743527989167,1.68975214452658,1.71736328225565,1.72150090272662,1.72399648681361,
1.72593038437794,1.72802423287369,1.73136453467282,1.74249734349255,1.7609215473519,
1.80769170426024,1.81239636126156,1.82702418612506,1.82935850623005,1.83075641110029,
1.83183541342338,1.83304457384182,1.83510136760709,1.84328361300178,1.85880947313267,
1.90026437117459,1.90568732077929,1.91248088503755,1.93024129957683,1.93391848720998,
1.9363016658098,1.93821746452181,1.94039729841907,1.94412577070548,1.9595735030194,
2.01117048502747,2.03856342563001,2.04146895397035,2.04285615362426,2.04393117427766,
2.04516075937704,2.04730956747509,2.0566828324811,2.10594454896407,2.14117115456242,
2.14546864018391,2.14801093363032,2.14995226745882,2.15202609326085,2.15527518228868,
2.16558396509852,2.18214115986211,2.21503010009364,2.25067402459901,2.25353929057919,
2.25491859956229,2.25599279730645,2.25722740238569,2.25939912693306,2.26909913043769,
2.31807663577105,2.35321663378768,2.35751286566527,2.36005474967951,2.36199596220488,
2.36406984394431,2.36731940794986,2.37763296236546,2.39420092671154,2.42791430094642,
2.46269184112862,2.4655709325517,2.46695291782961,2.46799572897164,2.46800048615618,
2.46800515994633,2.46800975198409,2.46801426420427,2.46801869840922,2.46802305638761,
2.46802733966539,2.46803154982998,2.46803568862605,2.46803975739891,2.46804375757856,
2.46804769072524,2.46805155828045,2.46805515525448,2.46805873875214,2.46806230882394,
2.46806586566859,2.46806940949222,2.46929342575355,2.47060523319878,2.47263011108784,
2.47644761109667,2.48573747155612,2.52373742824155,2.53838555562746,2.56552945305741,
2.56965537121082,2.57214764549138,2.57408120384947,2.57617690892246,2.57952499461605,
2.59072883132307,2.60931753906047,2.6683654535451),.UNSPECIFIED.);
#2043=B_SPLINE_CURVE_WITH_KNOTS('',3,(#202197,#202198,#202199,#202200,#202201,
#202202,#202203,#202204,#202205,#202206,#202207,#202208,#202209,#202210,
#202211,#202212,#202213,#202214,#202215,#202216,#202217,#202218),
 .UNSPECIFIED.,.F.,.F.,(4,2,2,2,2,2,2,2,2,2,4),(0.000810723293800813,0.00554261288036417,
0.00881069567732799,0.0102445757462057,0.0113189845998339,0.0123418012301504,
0.0133650032428226,0.0148060197505862,0.0186526214094667,0.0263910128961989,
0.0750776857911647),.UNSPECIFIED.);
#2044=B_SPLINE_CURVE_WITH_KNOTS('',3,(#202223,#202224,#202225,#202226,#202227,
#202228,#202229,#202230,#202231,#202232,#202233,#202234,#202235,#202236,
#202237,#202238,#202239,#202240,#202241,#202242,#202243,#202244,#202245,
#202246,#202247,#202248,#202249,#202250,#202251,#202252,#202253,#202254,
#202255,#202256,#202257,#202258,#202259,#202260,#202261,#202262,#202263,
#202264,#202265,#202266,#202267,#202268,#202269,#202270,#202271,#202272,
#202273,#202274,#202275,#202276,#202277,#202278,#202279,#202280,#202281,
#202282,#202283,#202284,#202285,#202286,#202287,#202288,#202289,#202290,
#202291,#202292,#202293,#202294,#202295,#202296,#202297,#202298,#202299,
#202300,#202301,#202302,#202303,#202304,#202305,#202306,#202307,#202308,
#202309,#202310,#202311,#202312,#202313,#202314,#202315,#202316,#202317,
#202318,#202319,#202320,#202321,#202322,#202323,#202324,#202325,#202326,
#202327,#202328,#202329,#202330,#202331,#202332,#202333,#202334,#202335,
#202336,#202337,#202338,#202339,#202340,#202341,#202342,#202343,#202344,
#202345,#202346,#202347,#202348,#202349,#202350,#202351,#202352,#202353,
#202354,#202355,#202356,#202357,#202358,#202359,#202360,#202361,#202362,
#202363,#202364,#202365,#202366,#202367,#202368,#202369,#202370,#202371,
#202372,#202373,#202374,#202375,#202376,#202377,#202378,#202379,#202380,
#202381,#202382,#202383,#202384,#202385,#202386,#202387,#202388,#202389,
#202390,#202391,#202392,#202393,#202394,#202395,#202396,#202397,#202398,
#202399,#202400,#202401,#202402,#202403,#202404,#202405,#202406,#202407,
#202408,#202409,#202410,#202411,#202412,#202413,#202414,#202415,#202416,
#202417,#202418,#202419,#202420,#202421,#202422,#202423,#202424,#202425,
#202426,#202427,#202428,#202429,#202430,#202431,#202432,#202433,#202434,
#202435,#202436,#202437,#202438,#202439,#202440,#202441,#202442,#202443,
#202444,#202445,#202446,#202447,#202448,#202449,#202450,#202451,#202452,
#202453,#202454),.UNSPECIFIED.,.F.,.F.,(4,2,2,2,2,2,2,2,2,2,2,2,2,2,2,2,
2,2,2,2,2,2,2,2,2,2,2,2,2,2,2,2,2,2,2,2,2,2,2,2,2,2,2,2,2,2,2,2,2,2,2,2,
2,2,2,2,2,2,2,2,2,2,2,2,2,2,2,2,2,2,2,2,2,2,2,2,2,2,2,2,2,2,2,2,2,2,2,2,
2,2,2,2,2,2,2,2,2,2,2,2,2,2,2,2,2,2,2,2,2,2,2,2,2,2,2,4),(1.25972979047866,
1.26441544661838,1.3053610613189,1.32784160728741,1.33050512980155,1.33184401796151,
1.33281203044151,1.33403568918917,1.33615828902696,1.34517733233056,1.36316313661643,
1.4133807127183,1.43118515687013,1.43486474854704,1.43724846399644,1.43916402554714,
1.44134286563753,1.44506784009828,1.46047491616359,1.51181204801717,1.53949164612553,
1.5423987079172,1.54378607016068,1.54486095401903,1.54609008841637,1.54823741794453,
1.55759346836069,1.60686081724013,1.64208553053703,1.64638235700535,1.6489242455072,
1.65086526147395,1.65293873934485,1.65618726577919,1.66649411625969,1.6830480673437,
1.71593115656945,1.7293786806246,1.73696339845124,1.75196165556578,1.75431125715591,
1.75571350569481,1.75679293741798,1.75799933084553,1.7600442820177,1.76808819268639,
1.78322781985062,1.82293120494068,1.85417110674922,1.85839662823766,1.86091774065261,
1.86285534853089,1.86493737621978,1.86822502090342,1.8788782170039,1.89620582015083,
1.94441101571001,1.94870738494384,1.95125573763788,1.96413443037342,1.96638353439067,
1.96777099166722,1.96884584752657,1.97007483613716,1.97222164393327,1.98157126688385,
2.03084192735482,2.0660667153899,2.07036338620625,2.07290517686419,2.07484611479717,
2.07691950609162,2.08016789016946,2.09047423240022,2.10702731337179,2.13990890153686,
2.1533392808224,2.16096715021381,2.17594022523108,2.17828871779687,2.17969061312604,
2.18076996043251,2.18197646777555,2.184022068518,2.19207431895256,2.20723746151434,
2.24809402712651,2.27819036368754,2.2823904040134,2.28490402384112,2.28684038669099,
2.28892552206687,2.29222753760886,2.30301126794517,2.32063481327829,2.36540042647044,
2.37279931702476,2.3780325514617,2.38836987511231,2.39047057420638,2.39181291642993,
2.39288397540113,2.39414472195357,2.39643695913237,2.40809259323571,2.45644047193006,
2.49005757649922,2.49432866384189,2.49686296032778,2.49880259141716,2.50087888167573,
2.50396415646811,2.51344816507387,2.52832065029717,2.55076555222504,2.59331776226468),
 .UNSPECIFIED.);
#2045=B_SPLINE_CURVE_WITH_KNOTS('',3,(#202455,#202456,#202457,#202458,#202459,
#202460,#202461,#202462,#202463,#202464,#202465,#202466,#202467,#202468,
#202469,#202470,#202471,#202472,#202473,#202474,#202475,#202476,#202477,
#202478,#202479,#202480,#202481,#202482,#202483,#202484,#202485,#202486,
#202487,#202488,#202489,#202490,#202491,#202492,#202493,#202494,#202495,
#202496,#202497,#202498,#202499,#202500,#202501,#202502,#202503,#202504,
#202505,#202506,#202507,#202508,#202509,#202510,#202511,#202512,#202513,
#202514,#202515,#202516,#202517,#202518,#202519,#202520,#202521,#202522,
#202523,#202524,#202525,#202526,#202527,#202528,#202529,#202530,#202531,
#202532,#202533,#202534,#202535,#202536,#202537,#202538,#202539,#202540,
#202541,#202542,#202543,#202544,#202545,#202546,#202547,#202548,#202549,
#202550,#202551,#202552,#202553,#202554,#202555,#202556,#202557,#202558,
#202559,#202560,#202561,#202562,#202563,#202564,#202565,#202566,#202567,
#202568,#202569,#202570,#202571,#202572,#202573,#202574,#202575,#202576,
#202577,#202578,#202579,#202580,#202581,#202582,#202583,#202584,#202585,
#202586,#202587,#202588,#202589,#202590,#202591,#202592,#202593,#202594,
#202595,#202596,#202597,#202598,#202599,#202600,#202601,#202602,#202603,
#202604,#202605,#202606,#202607,#202608,#202609,#202610,#202611,#202612,
#202613,#202614,#202615,#202616,#202617,#202618,#202619,#202620,#202621,
#202622,#202623,#202624,#202625,#202626,#202627,#202628,#202629,#202630,
#202631,#202632,#202633,#202634,#202635,#202636,#202637,#202638,#202639,
#202640,#202641,#202642,#202643,#202644,#202645,#202646,#202647,#202648,
#202649,#202650,#202651,#202652,#202653,#202654,#202655,#202656,#202657,
#202658,#202659,#202660,#202661,#202662,#202663,#202664,#202665,#202666,
#202667,#202668,#202669,#202670,#202671,#202672,#202673,#202674,#202675,
#202676,#202677,#202678,#202679,#202680,#202681,#202682,#202683,#202684,
#202685,#202686,#202687,#202688,#202689,#202690,#202691,#202692),
 .UNSPECIFIED.,.F.,.F.,(4,2,2,2,2,2,2,2,2,2,2,2,2,2,2,2,2,2,2,2,2,2,2,2,
2,2,2,2,2,2,2,2,2,2,2,2,2,2,2,2,2,2,2,2,2,2,2,2,2,2,2,2,2,2,2,2,2,2,2,2,
2,2,2,2,2,2,2,2,2,2,2,2,2,2,2,2,2,2,2,2,2,2,2,2,2,2,2,2,2,2,2,2,2,2,2,2,
2,2,2,2,2,2,2,2,2,2,2,2,2,2,2,2,2,2,2,2,2,2,4),(0.0750776857911647,0.0854662128806517,
0.102113513010209,0.112462472456125,0.115715011359714,0.117788838543863,
0.119728630399909,0.122266681563765,0.126552051773031,0.169578646218511,
0.206314577630255,0.21544505052592,0.219215482639955,0.221222238265942,
0.222526258215038,0.223741864100537,0.224784482334952,0.226132418959838,
0.228755851296678,0.244846643278332,0.279928082166132,0.308528693246175,
0.323516269928108,0.32720807634895,0.329379151199865,0.331294981377584,
0.333688364679299,0.337400697434074,0.355733226600146,0.400166554420321,
0.422006851272112,0.432208086194616,0.434412653047945,0.435654098356039,
0.436726766395204,0.438094390116348,0.440902368864504,0.461852212431691,
0.508438144622218,0.532022390876901,0.537812874490773,0.540408818687665,
0.542350850112764,0.544170007538085,0.546684082903521,0.553153512053729,
0.610547729454446,0.63360267901706,0.644148564382533,0.646375206844844,
0.64762153109111,0.648693701157503,0.65005461102966,0.652216513321899,0.66352505516041,
0.667420965350106,0.675166234930583,0.688551738819603,0.721403415187081,
0.744143066111857,0.749821033615603,0.752396643121415,0.754335628674015,
0.756160833714146,0.75869747484129,0.765305818218002,0.821458408085833,
0.845317348858873,0.856084653013628,0.85832513359427,0.859574557371751,
0.860646518783183,0.862003470709962,0.86466817254514,0.881842551046938,
0.927336280123037,0.955192998759887,0.961524797529677,0.964216189288776,
0.966174748980582,0.967971007649691,0.970856013044009,0.977862144219322,
1.02919750989356,1.05636664255927,1.06798908640502,1.07027941596559,1.07153970300641,
1.07261072957908,1.07395347920677,1.0765519918091,1.09206281584894,1.09863713189724,
1.1400150245994,1.16727980036919,1.17353960115029,1.17621873185625,1.1781751753605,
1.17997423290247,1.18287419811612,1.18996967520648,1.23959823919283,1.27797520449599,
1.28156104996634,1.28307197542321,1.28416446040919,1.28518984720792,1.28693024629093,
1.29164521912667,1.3320546855614,1.33394409779729,1.3777690553888,1.38499098155144,
1.38791221156124,1.38971522305868,1.39166870674747,1.39433074808804,1.40049146476992,
1.40843319572732),.UNSPECIFIED.);
#2046=B_SPLINE_CURVE_WITH_KNOTS('',3,(#202698,#202699,#202700,#202701),
 .UNSPECIFIED.,.F.,.F.,(4,4),(152.105783788367,152.455231388399),
 .UNSPECIFIED.);
#2047=B_SPLINE_CURVE_WITH_KNOTS('',3,(#202702,#202703,#202704,#202705,#202706,
#202707,#202708,#202709,#202710,#202711,#202712,#202713,#202714,#202715,
#202716,#202717,#202718,#202719,#202720,#202721,#202722,#202723,#202724,
#202725,#202726,#202727,#202728,#202729,#202730,#202731,#202732,#202733,
#202734,#202735,#202736,#202737,#202738,#202739,#202740,#202741,#202742,
#202743,#202744,#202745,#202746,#202747,#202748,#202749,#202750,#202751,
#202752,#202753,#202754,#202755,#202756,#202757,#202758,#202759,#202760,
#202761,#202762,#202763,#202764,#202765,#202766,#202767,#202768,#202769,
#202770,#202771,#202772,#202773,#202774,#202775,#202776,#202777,#202778,
#202779,#202780,#202781,#202782,#202783,#202784,#202785,#202786,#202787,
#202788,#202789,#202790,#202791,#202792,#202793,#202794,#202795,#202796,
#202797,#202798,#202799,#202800,#202801,#202802,#202803,#202804,#202805,
#202806,#202807,#202808,#202809,#202810,#202811,#202812,#202813,#202814,
#202815,#202816,#202817,#202818,#202819,#202820,#202821,#202822,#202823,
#202824,#202825,#202826,#202827,#202828,#202829,#202830,#202831,#202832,
#202833,#202834,#202835,#202836,#202837,#202838,#202839,#202840,#202841,
#202842,#202843,#202844,#202845,#202846,#202847,#202848,#202849,#202850,
#202851,#202852,#202853,#202854,#202855,#202856,#202857,#202858,#202859,
#202860,#202861,#202862,#202863,#202864,#202865,#202866,#202867,#202868,
#202869,#202870,#202871,#202872,#202873,#202874,#202875,#202876,#202877,
#202878,#202879,#202880,#202881,#202882,#202883,#202884,#202885,#202886,
#202887,#202888,#202889,#202890,#202891,#202892,#202893,#202894,#202895,
#202896,#202897,#202898,#202899,#202900,#202901,#202902,#202903,#202904,
#202905,#202906,#202907,#202908,#202909,#202910,#202911),.UNSPECIFIED.,
 .F.,.F.,(4,2,2,2,2,2,2,2,2,2,2,2,2,2,2,2,2,2,2,2,2,2,2,2,2,2,2,2,2,2,2,
2,2,2,2,2,2,2,2,2,2,2,2,2,2,2,2,2,2,2,2,2,2,2,2,2,2,2,2,2,2,2,2,2,2,2,2,
2,2,2,2,2,2,2,2,2,2,2,2,2,2,2,2,2,2,2,2,2,2,2,2,2,2,2,2,2,2,2,2,2,2,2,2,
2,4),(0.000629313894772825,0.0163201057884129,0.0544201859933447,0.058003511077306,
0.0595138340669082,0.0606060551084784,0.0616313308680476,0.0633718331634841,
0.0680887831680241,0.112806259851638,0.13693201608523,0.151520373459769,
0.160861098942264,0.163933559753649,0.166006632046877,0.167947109366619,
0.170488064305094,0.174782833329962,0.209904581901936,0.258831998605639,
0.268597987373947,0.27077373873528,0.272008963729442,0.273082636513288,
0.274459870255308,0.277316013071211,0.300127821126255,0.345794510276056,
0.362353003017357,0.372662406694839,0.37591082752992,0.377984025652916,
0.379924631118862,0.382465768811906,0.386760880245431,0.421889856834204,
0.470835662474782,0.480584246911095,0.482758903857259,0.483993937037209,
0.485067718214192,0.486445450690249,0.489303866086973,0.525387805716559,
0.558081158061455,0.580569801177691,0.586214163995462,0.588783792192102,
0.590722045777741,0.592549333440548,0.595093317229995,0.601747175732378,
0.657468429688583,0.681617892032286,0.692464258824482,0.694709737579719,
0.695960345083562,0.697032333501087,0.698388051759229,0.700532391059881,
0.71154838607147,0.762828588164124,0.791475767664967,0.797902873859704,
0.800610610486495,0.802572270015877,0.80436531139643,0.807231921514496,
0.814125449677963,0.867130606206088,0.893123385419549,0.904452259754445,
0.906726188400712,0.907982999434976,0.909054432270387,0.910401965547792,
0.913022257816694,0.929039407105128,0.929690928185521,0.974004119802603,
1.00337474986631,1.00988765092338,1.01260988419403,1.01457426067376,1.0163644561045,
1.01921498407812,1.0260105189294,1.08022203964785,1.10538729233139,1.11650314549799,
1.11876478978648,1.12001896803965,1.12109069161044,1.12244182620981,1.12507868313549,
1.14151014293562,1.19210040090442,1.20981256340647,1.22063658528523,1.2239432024748,
1.22602946922786,1.22796566111022,1.23047733012731,1.23467034641304,1.25972979047866),
 .UNSPECIFIED.);
#2048=B_SPLINE_CURVE_WITH_KNOTS('',3,(#202913,#202914,#202915,#202916,#202917,
#202918,#202919,#202920,#202921,#202922,#202923,#202924,#202925,#202926,
#202927,#202928,#202929,#202930,#202931,#202932,#202933,#202934,#202935,
#202936,#202937,#202938,#202939,#202940,#202941,#202942,#202943,#202944,
#202945,#202946,#202947,#202948,#202949,#202950,#202951,#202952,#202953,
#202954,#202955,#202956,#202957,#202958,#202959,#202960,#202961,#202962,
#202963,#202964,#202965,#202966,#202967,#202968,#202969,#202970,#202971,
#202972,#202973,#202974,#202975,#202976,#202977,#202978,#202979,#202980,
#202981,#202982,#202983,#202984,#202985,#202986,#202987,#202988,#202989,
#202990,#202991,#202992,#202993,#202994,#202995,#202996,#202997,#202998,
#202999,#203000,#203001,#203002,#203003,#203004,#203005,#203006,#203007,
#203008,#203009,#203010,#203011,#203012,#203013,#203014,#203015,#203016,
#203017,#203018,#203019,#203020,#203021,#203022,#203023,#203024,#203025,
#203026,#203027,#203028,#203029,#203030,#203031,#203032,#203033,#203034,
#203035,#203036,#203037,#203038,#203039,#203040,#203041,#203042,#203043,
#203044,#203045,#203046,#203047,#203048,#203049,#203050,#203051,#203052,
#203053,#203054,#203055,#203056,#203057,#203058,#203059,#203060,#203061,
#203062,#203063,#203064,#203065,#203066,#203067,#203068,#203069,#203070,
#203071,#203072,#203073,#203074,#203075,#203076,#203077,#203078,#203079,
#203080,#203081,#203082,#203083,#203084,#203085,#203086,#203087,#203088,
#203089,#203090,#203091,#203092,#203093,#203094,#203095,#203096,#203097,
#203098,#203099,#203100,#203101,#203102,#203103,#203104,#203105,#203106,
#203107,#203108,#203109,#203110,#203111,#203112,#203113,#203114,#203115,
#203116,#203117,#203118,#203119,#203120,#203121,#203122,#203123,#203124,
#203125,#203126,#203127,#203128),.UNSPECIFIED.,.F.,.F.,(4,2,2,2,2,2,2,2,
2,2,2,2,2,2,2,2,2,2,2,2,2,2,2,2,2,2,2,2,2,2,2,2,2,2,2,2,2,2,2,2,2,2,2,2,
2,2,2,2,2,2,2,2,2,2,2,2,2,2,2,2,2,2,2,2,2,2,2,2,2,2,2,2,2,2,2,2,2,2,2,2,
2,2,2,2,2,2,2,2,2,2,2,2,2,2,2,2,2,2,2,2,2,2,2,2,2,2,2,4),(1.40843319572732,
1.42695731648832,1.46587333981965,1.47401635250847,1.49128931104146,1.49395781187334,
1.49531562368928,1.49638770882099,1.49763664550364,1.49987467007586,1.51060061965061,
1.53430394351945,1.56167608299342,1.59360626912867,1.59784576883013,1.60037091261219,
1.60230911167032,1.6043893183177,1.60766889029093,1.61825047610564,1.63541707716733,
1.68115614033856,1.68792200324815,1.70336678250791,1.70573464644326,1.70714221331575,
1.70822236916999,1.70942584279954,1.71145772380151,1.71934890486926,1.73406667207418,
1.76310493703932,1.80549050289223,1.8097835210629,1.81232423638252,1.8142649785188,
1.81633876714915,1.81958904046634,1.8299120618514,1.84650210602008,1.87941417023541,
1.89545412468211,1.89925794956622,1.91528181190017,1.91790235229976,1.91924988487568,
1.92032124917145,1.92157790678213,1.9238513616789,1.93517440363395,1.96114299568423,
2.01413424879559,2.02102544135396,2.02389154930304,2.02568441579992,2.0276460017689,
2.03035384504351,2.03678217404211,2.06544509919645,2.11674021308599,2.12775980409431,
2.12990435161104,2.13126010903991,2.13233207143994,2.13358258959672,2.13582774902764,
2.14666999949005,2.17080195418908,2.22650529605477,2.23315721559891,2.23570085203259,
2.23752802028449,2.23946626654463,2.24203608049835,2.24768163593029,2.27018211658393,
2.30291064292561,2.33898617511563,2.34184595819503,2.34322396051763,2.34429776587213,
2.34553262532202,2.34770648123255,2.35744366393611,2.40637342642948,2.44148699526411,
2.4461649031357,2.44859886023886,2.45046883506032,2.45255445190642,2.45473702611308,
2.45795216888837,2.49308193384322,2.54887914088592,2.55315894461639,2.55483153729244,
2.55584379223923,2.55694602488149,2.5585102056888,2.56241787407287,2.58158152562364,
2.64854564337416,2.65670852799325,2.65977977395676,2.66161107895188,2.66345503868571,
2.66574688078778,2.6678112172335),.UNSPECIFIED.);
#2049=B_SPLINE_CURVE_WITH_KNOTS('',3,(#203129,#203130,#203131,#203132,#203133,
#203134,#203135,#203136,#203137,#203138),.UNSPECIFIED.,.F.,.F.,(4,2,2,2,
4),(0.000823824276227816,0.00402823554000867,0.0105267000676126,0.0601103595096327,
0.0751122659302341),.UNSPECIFIED.);
#2050=B_SPLINE_CURVE_WITH_KNOTS('',3,(#203144,#203145,#203146,#203147,#203148,
#203149),.UNSPECIFIED.,.F.,.F.,(4,2,4),(2.59315592359719,2.60891630066588,
2.66742167112986),.UNSPECIFIED.);
#2051=B_SPLINE_CURVE_WITH_KNOTS('',3,(#203150,#203151,#203152,#203153,#203154,
#203155,#203156,#203157,#203158,#203159),.UNSPECIFIED.,.F.,.F.,(4,1,1,1,
1,1,1,4),(152.455231388399,152.821976844167,153.820813294129,154.81964974409,
155.818486194052,156.817322644014,157.816159093976,158.388969095546),
 .UNSPECIFIED.);
#2052=B_SPLINE_CURVE_WITH_KNOTS('',3,(#203160,#203161,#203162,#203163,#203164,
#203165,#203166,#203167,#203168,#203169,#203170,#203171,#203172,#203173,
#203174,#203175,#203176,#203177,#203178,#203179,#203180,#203181,#203182,
#203183,#203184,#203185,#203186,#203187,#203188,#203189,#203190,#203191,
#203192,#203193,#203194,#203195,#203196,#203197,#203198,#203199,#203200,
#203201,#203202,#203203,#203204,#203205,#203206,#203207,#203208,#203209,
#203210,#203211,#203212,#203213,#203214,#203215,#203216,#203217,#203218,
#203219,#203220,#203221,#203222,#203223,#203224,#203225,#203226,#203227,
#203228,#203229,#203230,#203231,#203232,#203233,#203234,#203235,#203236,
#203237,#203238,#203239,#203240,#203241,#203242,#203243,#203244,#203245,
#203246,#203247,#203248,#203249,#203250,#203251,#203252,#203253,#203254,
#203255,#203256,#203257,#203258,#203259,#203260,#203261,#203262,#203263,
#203264,#203265,#203266,#203267,#203268,#203269,#203270,#203271,#203272,
#203273,#203274,#203275,#203276,#203277,#203278,#203279,#203280,#203281,
#203282,#203283,#203284,#203285,#203286,#203287,#203288,#203289,#203290,
#203291,#203292,#203293,#203294,#203295,#203296,#203297,#203298,#203299,
#203300,#203301,#203302,#203303,#203304,#203305,#203306,#203307,#203308,
#203309,#203310,#203311,#203312,#203313,#203314,#203315,#203316,#203317,
#203318,#203319,#203320,#203321,#203322,#203323,#203324,#203325,#203326,
#203327,#203328,#203329,#203330,#203331,#203332,#203333,#203334,#203335,
#203336,#203337,#203338,#203339,#203340,#203341,#203342,#203343,#203344,
#203345,#203346,#203347,#203348,#203349,#203350,#203351,#203352,#203353,
#203354,#203355,#203356,#203357,#203358,#203359,#203360,#203361,#203362,
#203363,#203364,#203365,#203366,#203367,#203368,#203369,#203370,#203371,
#203372,#203373,#203374,#203375,#203376,#203377,#203378,#203379,#203380,
#203381,#203382,#203383,#203384,#203385,#203386,#203387,#203388,#203389,
#203390,#203391,#203392,#203393,#203394,#203395,#203396,#203397,#203398,
#203399,#203400,#203401,#203402,#203403,#203404,#203405,#203406,#203407,
#203408,#203409,#203410,#203411,#203412,#203413,#203414,#203415,#203416,
#203417,#203418,#203419,#203420,#203421,#203422,#203423,#203424,#203425,
#203426,#203427,#203428,#203429,#203430,#203431,#203432,#203433,#203434,
#203435),.UNSPECIFIED.,.F.,.F.,(4,2,2,2,2,2,2,2,2,2,2,2,2,2,2,2,2,2,2,2,
2,2,2,2,2,2,2,2,2,2,2,2,2,2,2,2,2,2,2,2,2,2,2,2,2,2,2,2,2,2,2,2,2,2,2,2,
2,2,2,2,2,2,2,2,2,2,2,2,2,2,2,2,2,2,2,2,2,2,2,2,2,2,2,2,2,2,2,2,2,2,2,2,
2,2,2,2,2,2,2,2,2,2,2,2,2,2,2,2,2,2,2,2,2,2,2,2,2,2,2,2,2,2,2,2,2,2,2,2,
2,2,2,2,2,2,2,2,2,4),(0.0751122659302341,0.085828878825592,0.0970868110481651,
0.0993563555451385,0.100612073461201,0.101683382847819,0.103031790709545,
0.10565681638989,0.121802814244195,0.172381098038625,0.190284662893531,
0.201191748518281,0.203647518624949,0.205928943311196,0.205943863292443,
0.205959399610425,0.205975593874828,0.205992491573063,0.206010142783773,
0.206028602703602,0.206047932242364,0.206068198973089,0.206089477926499,
0.206111852850056,0.206135417431713,0.206160276963575,0.206186550301097,
0.20621437210921,0.206243895752698,0.206275296862062,0.206308777602607,
0.206344572247025,0.20821731272881,0.210599717359116,0.215045795121062,
0.241166177948392,0.284929293597834,0.301025008859123,0.309405652452208,
0.311478260239731,0.31269067274794,0.313768460568666,0.315159440535809,
0.31747097912074,0.331619418740069,0.342238328607994,0.38562798519719,0.409018583727364,
0.414783744998917,0.417375305203036,0.419316841122738,0.421137558099361,
0.423656999570428,0.43015805816979,0.487280697079861,0.510517692195319,
0.521114646640081,0.523344682687182,0.524591849602223,0.525664087826453,
0.527024238510021,0.529703813501034,0.547289991057891,0.555090515258147,
0.565599528223832,0.598431611186449,0.614959756296749,0.625255709364678,
0.628502792552046,0.630575834651251,0.63251678438357,0.635059080611407,
0.63935773728141,0.674736803913771,0.723923619866213,0.733241115571108,
0.735385610659766,0.736614078190253,0.737689006812695,0.739077244557444,
0.741989039743823,0.773695991869402,0.777689021102544,0.810489725132012,
0.833142836239981,0.838809742899897,0.841383685350726,0.843322775963028,
0.845149077890299,0.847688842652357,0.854314735300919,0.910325837239713,
0.934291589604419,0.945088860945829,0.947331540212699,0.948581622742244,
0.949653799092122,0.951010573603945,0.953158118252572,0.964223221520589,
1.01536624081847,1.04409282272519,1.0505297317483,1.05323930695841,1.0552014672327,
1.05699439464595,1.0598595792886,1.06674323897249,1.11989293571659,1.14579229963293,
1.15709790249943,1.15937067895881,1.16062732651352,1.16169890755991,1.16304699331893,
1.16566943644532,1.18171826673186,1.18582956695817,1.20152232426753,1.23441215403954,
1.25720138141645,1.26288695609681,1.26546450453172,1.2674043374973,1.26922989156428,
1.27176629974413,1.27836983492409,1.33461082161945,1.35356472111645,1.36856797597223,
1.37091816755845,1.37232074623916,1.37340041866843,1.37460706603077,1.37665241518814,
1.38469748033816,1.39983872514726,1.40873148512311),.UNSPECIFIED.);
#2053=B_SPLINE_CURVE_WITH_KNOTS('',3,(#203440,#203441,#203442,#203443,#203444,
#203445,#203446,#203447,#203448,#203449,#203450,#203451,#203452,#203453,
#203454,#203455,#203456,#203457,#203458,#203459,#203460,#203461,#203462,
#203463,#203464,#203465,#203466,#203467,#203468,#203469,#203470,#203471,
#203472,#203473,#203474,#203475,#203476,#203477,#203478,#203479,#203480,
#203481,#203482,#203483,#203484,#203485,#203486,#203487,#203488,#203489,
#203490,#203491,#203492,#203493,#203494,#203495,#203496,#203497,#203498,
#203499,#203500,#203501,#203502,#203503,#203504,#203505,#203506,#203507,
#203508,#203509,#203510,#203511,#203512,#203513,#203514,#203515,#203516,
#203517,#203518,#203519,#203520,#203521,#203522,#203523,#203524,#203525,
#203526,#203527,#203528,#203529,#203530,#203531,#203532,#203533,#203534,
#203535,#203536,#203537,#203538,#203539,#203540,#203541,#203542,#203543,
#203544,#203545,#203546,#203547,#203548,#203549,#203550,#203551,#203552,
#203553,#203554,#203555,#203556,#203557,#203558,#203559,#203560,#203561,
#203562,#203563,#203564,#203565,#203566,#203567,#203568,#203569,#203570,
#203571,#203572,#203573,#203574,#203575,#203576,#203577,#203578,#203579,
#203580,#203581,#203582,#203583,#203584,#203585,#203586,#203587,#203588,
#203589,#203590,#203591,#203592,#203593,#203594,#203595,#203596,#203597,
#203598,#203599,#203600,#203601,#203602,#203603,#203604,#203605,#203606,
#203607,#203608,#203609,#203610,#203611,#203612,#203613,#203614,#203615,
#203616,#203617,#203618,#203619,#203620,#203621,#203622,#203623,#203624,
#203625,#203626,#203627,#203628,#203629,#203630,#203631,#203632,#203633,
#203634,#203635,#203636,#203637,#203638,#203639,#203640,#203641,#203642,
#203643,#203644,#203645,#203646,#203647,#203648,#203649,#203650,#203651,
#203652,#203653,#203654,#203655,#203656,#203657,#203658,#203659,#203660,
#203661,#203662,#203663,#203664,#203665,#203666,#203667,#203668,#203669,
#203670,#203671,#203672,#203673),.UNSPECIFIED.,.F.,.F.,(4,2,2,2,2,2,2,2,
2,2,2,2,2,2,2,2,2,2,2,2,2,2,2,2,2,2,2,2,2,2,2,2,2,2,2,2,2,2,2,2,2,2,2,2,
2,2,2,2,2,2,2,2,2,2,2,2,2,2,2,2,2,2,2,2,2,2,2,2,2,2,2,2,2,2,2,2,2,2,2,2,
2,2,2,2,2,2,2,2,2,2,2,2,2,2,2,2,2,2,2,2,2,2,2,2,2,2,2,2,2,2,2,2,2,2,2,2,
4),(1.25960927945369,1.26784056068535,1.29070305517887,1.30119586223981,
1.30341928562604,1.30466495514073,1.30573723667345,1.30709916579662,1.30978755174501,
1.32763514716263,1.33373204795653,1.37574263997476,1.40292854467451,1.40705404771045,
1.40954560847968,1.41147833629177,1.41357286270537,1.41691845713225,1.42810816167539,
1.44666703455994,1.49069774575448,1.49656843927689,1.51244824705574,1.51506158886226,
1.51640745051267,1.51747862366803,1.51873640767557,1.52101504423773,1.53242877663141,
1.5587556144553,1.61123418639183,1.61816335064033,1.62103577214087,1.62282983684166,
1.62479052775042,1.62749309914301,1.63388987746754,1.68178582156254,1.7213746982433,
1.72610769207243,1.72785089277105,1.72887687622625,1.72996904238941,1.73147806418142,
1.73505278632489,1.77424216861532,1.82298145965566,1.83011236861365,1.83301825935914,
1.83481840225398,1.8367739839029,1.83944824471868,1.84567976943025,1.87271784907334,
1.91343456524463,1.93614252156641,1.93899624933968,1.94037305645156,1.94144673945619,
1.94268236965753,1.94485976391051,1.95464886093963,2.00353430065314,2.03864073873109,
2.04293543194623,2.04547649278712,2.04741712656729,2.04949043819454,2.05273920904223,
2.06305108153262,2.07961711155464,2.11250738363383,2.1270680362877,2.13238492367237,
2.14842385062004,2.1510451305138,2.15239273736957,2.15346400855855,2.15472038501481,
2.15699285603943,2.16830127058305,2.19421412126112,2.24727753742218,2.25416201565285,
2.25702687422792,2.25881940752266,2.26078098958741,2.26348948923292,2.26992251464575,
2.29862707764436,2.3498476032982,2.3608812297336,2.36302652803489,2.36438245774963,
2.36545435010505,2.36670454699238,2.36894855284607,2.37977416098886,2.40384585326639,
2.45963485770822,2.46627520364442,2.46881688665781,2.47064342899255,2.4725194430492,
2.47500336289316,2.47774110006639,2.48229185387961,2.49161991296542,2.54225956213082,
2.57203621327389,2.57495058484101,2.57633919796764,2.57741402116202,2.57864193453782,
2.58078443077413,2.59007761168861,2.59315592359719),.UNSPECIFIED.);
#2054=B_SPLINE_CURVE_WITH_KNOTS('',3,(#203675,#203676,#203677,#203678,#203679,
#203680,#203681,#203682,#203683,#203684,#203685,#203686,#203687,#203688,
#203689,#203690,#203691,#203692,#203693,#203694,#203695,#203696,#203697,
#203698,#203699,#203700,#203701,#203702,#203703,#203704,#203705,#203706,
#203707,#203708,#203709,#203710,#203711,#203712,#203713,#203714,#203715,
#203716,#203717,#203718,#203719,#203720,#203721,#203722,#203723,#203724,
#203725,#203726,#203727,#203728,#203729,#203730,#203731,#203732,#203733,
#203734,#203735,#203736,#203737,#203738,#203739,#203740,#203741,#203742,
#203743,#203744,#203745,#203746,#203747,#203748,#203749,#203750,#203751,
#203752,#203753,#203754,#203755,#203756,#203757,#203758,#203759,#203760,
#203761,#203762,#203763,#203764,#203765,#203766,#203767,#203768,#203769,
#203770,#203771,#203772,#203773,#203774,#203775,#203776,#203777,#203778,
#203779,#203780,#203781,#203782,#203783,#203784,#203785,#203786,#203787,
#203788,#203789,#203790,#203791,#203792,#203793,#203794,#203795,#203796,
#203797,#203798,#203799,#203800,#203801,#203802,#203803,#203804,#203805,
#203806,#203807,#203808,#203809,#203810,#203811,#203812,#203813,#203814,
#203815,#203816,#203817,#203818,#203819,#203820,#203821,#203822,#203823,
#203824,#203825,#203826,#203827,#203828,#203829,#203830,#203831,#203832,
#203833,#203834,#203835,#203836,#203837,#203838,#203839,#203840,#203841,
#203842,#203843,#203844,#203845,#203846,#203847,#203848,#203849,#203850,
#203851,#203852,#203853,#203854,#203855,#203856,#203857,#203858,#203859,
#203860,#203861,#203862,#203863,#203864,#203865,#203866,#203867,#203868,
#203869,#203870,#203871,#203872,#203873,#203874,#203875,#203876,#203877,
#203878,#203879,#203880,#203881,#203882,#203883,#203884,#203885,#203886,
#203887,#203888,#203889,#203890,#203891,#203892,#203893,#203894,#203895,
#203896,#203897,#203898),.UNSPECIFIED.,.F.,.F.,(4,2,2,2,2,2,2,2,2,2,2,2,
2,2,2,2,2,2,2,2,2,2,2,2,2,2,2,2,2,2,2,2,2,2,2,2,2,2,2,2,2,2,2,2,2,2,2,2,
2,2,2,2,2,2,2,2,2,2,2,2,2,2,2,2,2,2,2,2,2,2,2,2,2,2,2,2,2,2,2,2,2,2,2,2,
2,2,2,2,2,2,2,2,2,2,2,2,2,2,2,2,2,2,2,2,2,2,2,2,2,2,2,4),(1.40873148512311,
1.43954141038742,1.47079962802823,1.47502632051913,1.47754805802225,1.47948610340675,
1.4815685590938,1.48485679029968,1.49551110179774,1.51283974492747,1.55312800056793,
1.58012246481206,1.58302494697855,1.58441154160231,1.58548648574311,1.58671642281291,
1.58886687965066,1.5982634941122,1.64750384981752,1.6827241502224,1.68702149907781,
1.68956373353539,1.69150503492834,1.69357883830035,1.69682791768685,1.70713688465068,
1.72369458008402,1.75658366016653,1.77013897321832,1.77745269684894,1.78179090962933,
1.79297526494844,1.79513021280011,1.7964892638977,1.79756164775093,1.79881015301174,
1.80104546560828,1.81172187639829,1.8352408649652,1.89190053299344,1.89845482549405,
1.90098324363558,1.90280660268653,1.90474739266829,1.90733183552432,1.9130557756659,
1.93613505434352,1.96966870742379,1.99211409908916,2.00484619071758,2.0070877605922,
2.00847297320677,2.00954762509103,2.01077810063698,2.0129315592425,2.02237367369485,
2.07156495933937,2.10676763193365,2.11106412780525,2.1136059029602,2.11554687968838,
2.11762036148754,2.12086898972392,2.13117696796551,2.14773349155529,2.18061848600975,
2.21625346366134,2.21911651538686,2.22049524404451,2.22156921712478,2.22280381975302,
2.22497615127895,2.23468888175323,2.28364516430624,2.31877576290163,2.32307119649038,
2.32561261931894,2.32755348597996,2.32962700433937,2.33287601171029,2.34318790662308,
2.35975331282198,2.3912034672034,2.42829559713972,2.43113341468106,2.43250716066688,
2.433580642496,2.43479364705273,2.43689635354939,2.43949336807867,2.44490278294649,
2.46031812615432,2.50136047554929,2.53093500282094,2.53512497338509,2.53763570477168,
2.53957168392176,2.54165822449844,2.54496634977607,2.55580486074104,2.57355287739486,
2.61947634618228,2.6278080198572,2.64081332124416,2.64306886678551,2.64445824632581,
2.64553327890896,2.64654209452073,2.64775526287028,2.64954167370693,2.65527690517876,
2.6679454068061),.UNSPECIFIED.);
#2055=B_SPLINE_CURVE_WITH_KNOTS('',3,(#203899,#203900,#203901,#203902,#203903,
#203904,#203905,#203906,#203907,#203908,#203909,#203910,#203911),
 .UNSPECIFIED.,.F.,.F.,(4,3,3,3,4),(-161.271232394665,-161.16946618359,
-161.067655474371,-160.965693995851,-160.920671713183),.UNSPECIFIED.);
#2056=B_SPLINE_CURVE_WITH_KNOTS('',3,(#203917,#203918,#203919,#203920,#203921,
#203922,#203923,#203924,#203925,#203926,#203927,#203928,#203929),
 .UNSPECIFIED.,.F.,.F.,(4,3,3,3,4),(170.955339710339,171.057208845626,171.158971098887,
171.260660137299,171.305836600057),.UNSPECIFIED.);
#2057=B_SPLINE_CURVE_WITH_KNOTS('',3,(#203930,#203931,#203932,#203933,#203934,
#203935,#203936,#203937,#203938,#203939,#203940,#203941,#203942,#203943,
#203944,#203945,#203946,#203947,#203948,#203949,#203950,#203951,#203952,
#203953,#203954,#203955,#203956,#203957,#203958,#203959,#203960,#203961,
#203962,#203963,#203964,#203965,#203966,#203967,#203968,#203969,#203970,
#203971,#203972,#203973,#203974,#203975,#203976,#203977,#203978,#203979,
#203980,#203981,#203982,#203983,#203984,#203985,#203986,#203987,#203988,
#203989,#203990,#203991,#203992,#203993,#203994,#203995,#203996,#203997,
#203998,#203999,#204000,#204001,#204002,#204003,#204004,#204005,#204006,
#204007,#204008,#204009,#204010,#204011,#204012,#204013,#204014,#204015,
#204016,#204017,#204018,#204019,#204020,#204021,#204022,#204023,#204024,
#204025,#204026,#204027,#204028,#204029,#204030,#204031,#204032,#204033,
#204034,#204035,#204036,#204037,#204038,#204039,#204040,#204041,#204042,
#204043,#204044,#204045,#204046,#204047,#204048,#204049,#204050,#204051,
#204052,#204053,#204054,#204055,#204056,#204057,#204058,#204059,#204060,
#204061,#204062,#204063,#204064,#204065,#204066,#204067,#204068,#204069,
#204070,#204071,#204072,#204073,#204074,#204075,#204076,#204077,#204078,
#204079,#204080,#204081,#204082,#204083,#204084,#204085,#204086,#204087,
#204088,#204089,#204090,#204091,#204092,#204093,#204094,#204095,#204096,
#204097,#204098,#204099,#204100,#204101,#204102,#204103,#204104,#204105,
#204106,#204107,#204108,#204109,#204110,#204111,#204112,#204113,#204114,
#204115,#204116,#204117,#204118,#204119,#204120,#204121,#204122,#204123,
#204124,#204125,#204126,#204127,#204128,#204129,#204130,#204131,#204132,
#204133,#204134,#204135,#204136,#204137,#204138,#204139,#204140,#204141,
#204142,#204143,#204144,#204145,#204146,#204147,#204148,#204149,#204150,
#204151),.UNSPECIFIED.,.F.,.F.,(4,2,2,2,2,2,2,2,2,2,2,2,2,2,2,2,2,2,2,2,
2,2,2,2,2,2,2,2,2,2,2,2,2,2,2,2,2,2,2,2,2,2,2,2,2,2,2,2,2,2,2,2,2,2,2,2,
2,2,2,2,2,2,2,2,2,2,2,2,2,2,2,2,2,2,2,2,2,2,2,2,2,2,2,2,2,2,2,2,2,2,2,2,
2,2,2,2,2,2,2,2,2,2,2,2,2,2,2,2,2,2,4),(0.000655555487746406,0.0215326867220369,
0.0285521057207997,0.0303960777145486,0.0316335698167745,0.0326484404410412,
0.0337175254276835,0.0350634362659286,0.0377855770018737,0.0559574692004484,
0.061638161908966,0.0739378941501972,0.0845184776971982,0.106384522445289,
0.122977092814764,0.133286052670248,0.136520215528419,0.138580655542259,
0.140506662082009,0.143024731538882,0.147271552045667,0.192337636321466,
0.220917652812677,0.234451027551801,0.241869026835945,0.243841420654799,
0.244851141182566,0.245918180059928,0.247244796379088,0.249294128909632,
0.258883142395294,0.318505419951983,0.335297078770584,0.345718786023299,
0.348984818510775,0.351065107730897,0.353009480963641,0.355551477179388,
0.359839182118602,0.39423280182301,0.443435079782813,0.453287138480796,
0.455474742211183,0.456715723135277,0.457791987620055,0.459170643306667,
0.462028507550171,0.48480471709289,0.527329230071651,0.545904435004286,
0.557102170076887,0.560449685950735,0.562545350531582,0.564479092283313,
0.566971916582978,0.571099442096233,0.598278238353839,0.640348116479544,
0.65690820639345,0.665449594930443,0.667534919720363,0.668750047887287,
0.669826498733916,0.671211235833482,0.673503643660504,0.687287896422153,
0.698621228031735,0.737949806914923,0.764492324349816,0.770660377970032,
0.773322016361416,0.775273840198162,0.777074356311094,0.779989358629309,
0.787184867462303,0.833862611011882,0.856213838851044,0.870037675624283,
0.875062793485331,0.878645311342973,0.880154605271385,0.881246040641265,
0.882271325117263,0.884011299816394,0.888723661899274,0.929075125968494,
0.977359006375441,0.982966744880172,0.985530002193917,0.98746767807645,
0.989297544767694,0.991850158636646,0.998557347295345,1.05366058603572,
1.0781766973765,1.08912118873027,1.09137328663972,1.09262570343644,1.09369780423249,
1.095051993725,1.09779133469493,1.11614973897311,1.16514968613826,1.18898302761693,
1.19480674987626,1.19740895638714,1.19935224745615,1.20117010545591,1.20367846665727,
1.2101117363724,1.25960927945369),.UNSPECIFIED.);
#2058=B_SPLINE_CURVE_WITH_KNOTS('',3,(#204153,#204154,#204155,#204156,#204157,
#204158,#204159,#204160,#204161,#204162,#204163,#204164,#204165,#204166,
#204167,#204168,#204169,#204170,#204171,#204172,#204173,#204174,#204175,
#204176,#204177,#204178,#204179,#204180,#204181,#204182,#204183,#204184,
#204185,#204186,#204187,#204188,#204189,#204190,#204191,#204192,#204193,
#204194,#204195,#204196,#204197,#204198,#204199,#204200,#204201,#204202,
#204203,#204204,#204205,#204206,#204207,#204208,#204209,#204210,#204211,
#204212,#204213,#204214,#204215,#204216,#204217,#204218,#204219,#204220,
#204221,#204222,#204223,#204224,#204225,#204226,#204227,#204228,#204229,
#204230,#204231,#204232,#204233,#204234,#204235,#204236,#204237,#204238,
#204239,#204240,#204241,#204242,#204243,#204244,#204245,#204246,#204247,
#204248,#204249,#204250,#204251,#204252,#204253,#204254,#204255,#204256,
#204257,#204258,#204259,#204260,#204261,#204262,#204263,#204264,#204265,
#204266,#204267,#204268,#204269,#204270,#204271,#204272,#204273,#204274,
#204275,#204276,#204277,#204278,#204279,#204280,#204281,#204282,#204283,
#204284,#204285,#204286,#204287,#204288,#204289,#204290,#204291,#204292,
#204293,#204294,#204295,#204296,#204297,#204298,#204299,#204300,#204301,
#204302,#204303,#204304,#204305,#204306,#204307,#204308,#204309,#204310,
#204311,#204312,#204313,#204314,#204315,#204316,#204317,#204318,#204319,
#204320,#204321,#204322,#204323,#204324,#204325,#204326,#204327,#204328,
#204329,#204330,#204331,#204332,#204333),.UNSPECIFIED.,.F.,.F.,(4,3,3,3,
3,3,3,3,3,3,3,3,3,3,3,3,3,3,3,3,3,3,3,3,3,3,3,3,3,3,3,3,3,3,3,3,3,3,3,3,
3,3,3,3,3,3,3,3,3,3,3,3,3,3,3,3,3,3,3,3,4),(-167.203857019737,-167.089811010942,
-166.97534442206,-166.860315018448,-166.805687143633,-166.70228742583,-166.59904112641,
-166.495916113768,-166.392856482536,-166.289828202843,-166.186797287972,
-166.083659483083,-165.980465364832,-165.877088418964,-165.806850693671,
-165.703453682928,-165.600210070056,-165.497087699756,-165.394030682219,
-165.291004983628,-165.187976613287,-165.084841278379,-164.981649592209,
-164.878274989697,-164.808014243709,-164.704622124948,-164.601383502989,
-164.498266247439,-164.395214418258,-164.292193974136,-164.189170916953,
-164.086040949216,-163.982854668774,-163.879485474421,-163.809177793747,
-163.705782197978,-163.602540048974,-163.499419208732,-163.396363761232,
-163.293339670433,-163.190312943454,-163.08717929565,-162.983989323685,
-162.880616460327,-162.810341343785,-162.706946384013,-162.603704872483,
-162.500584668762,-162.397529856858,-162.294506399785,-162.19148030372,
-162.088347278056,-161.985157924285,-161.881785665815,-161.811504893824,
-161.709471728966,-161.607582178419,-161.505807285033,-161.404097846253,
-161.302405175455,-161.271232394665),.UNSPECIFIED.);
#2059=B_SPLINE_CURVE_WITH_KNOTS('',3,(#204334,#204335,#204336,#204337,#204338,
#204339,#204340,#204341,#204342,#204343,#204344,#204345,#204346),
 .UNSPECIFIED.,.F.,.F.,(4,3,3,3,4),(-167.55333770454,-167.448855755634,
-167.344457480827,-167.240110523684,-167.203857020092),.UNSPECIFIED.);
#2060=B_SPLINE_CURVE_WITH_KNOTS('',3,(#204349,#204350,#204351,#204352,#204353,
#204354,#204355,#204356,#204357,#204358,#204359,#204360,#204361,#204362,
#204363,#204364,#204365,#204366,#204367,#204368,#204369,#204370,#204371,
#204372,#204373,#204374,#204375,#204376,#204377,#204378,#204379,#204380,
#204381,#204382,#204383,#204384,#204385,#204386,#204387,#204388,#204389,
#204390,#204391,#204392,#204393,#204394,#204395,#204396,#204397,#204398,
#204399,#204400,#204401,#204402,#204403,#204404,#204405,#204406,#204407,
#204408,#204409,#204410,#204411,#204412,#204413,#204414,#204415,#204416,
#204417,#204418,#204419,#204420,#204421,#204422,#204423,#204424,#204425,
#204426,#204427,#204428,#204429,#204430,#204431,#204432,#204433,#204434,
#204435,#204436,#204437,#204438,#204439,#204440,#204441,#204442,#204443,
#204444,#204445,#204446,#204447,#204448,#204449,#204450,#204451,#204452,
#204453,#204454,#204455,#204456,#204457,#204458,#204459,#204460,#204461,
#204462,#204463,#204464,#204465,#204466,#204467,#204468,#204469,#204470,
#204471,#204472,#204473,#204474,#204475,#204476,#204477,#204478,#204479,
#204480,#204481,#204482,#204483,#204484,#204485,#204486,#204487,#204488,
#204489,#204490,#204491,#204492,#204493,#204494,#204495,#204496,#204497,
#204498,#204499,#204500,#204501,#204502,#204503,#204504,#204505,#204506,
#204507,#204508),.UNSPECIFIED.,.F.,.F.,(4,3,3,3,3,3,3,3,3,3,3,3,3,3,3,3,
3,3,3,3,3,3,3,3,3,3,3,3,3,3,3,3,3,3,3,3,3,3,3,3,3,3,3,3,3,3,3,3,3,3,3,3,
3,4),(-172.787594225567,-172.684274861804,-172.581108909343,-172.478064373147,
-172.375085039686,-172.272136763294,-172.169185441327,-172.066129317591,
-171.963016197798,-171.859726812786,-171.799869393442,-171.696296438965,
-171.592873179124,-171.489566512639,-171.386322438044,-171.283107200028,
-171.179887083779,-171.076557935617,-170.973170984353,-170.869600941516,
-170.80103294348,-170.697770604844,-170.594663628611,-170.491680177536,
-170.388763416087,-170.285879110466,-170.182993071298,-170.080000538274,
-169.976952142771,-169.873720029761,-169.802196493519,-169.698775165844,
-169.595507193078,-169.492360519935,-169.389279247763,-169.286229378952,
-169.183176959081,-169.080017930163,-168.97680271242,-168.873405104616,
-168.803360043557,-168.69994450726,-168.59668195947,-168.493540133569,-168.390463349949,
-168.287417603378,-168.184368931446,-168.081213043256,-167.978000631122,
-167.874605253038,-167.804523593595,-167.699655949217,-167.594982598059,
-167.55333770454),.UNSPECIFIED.);
#2061=B_SPLINE_CURVE_WITH_KNOTS('',3,(#204511,#204512,#204513,#204514,#204515,
#204516,#204517,#204518,#204519,#204520,#204521,#204522,#204523,#204524,
#204525,#204526,#204527,#204528,#204529,#204530,#204531,#204532,#204533,
#204534,#204535,#204536,#204537,#204538,#204539,#204540,#204541,#204542,
#204543,#204544,#204545,#204546,#204547,#204548,#204549,#204550,#204551,
#204552,#204553,#204554,#204555,#204556,#204557,#204558,#204559,#204560,
#204561,#204562,#204563,#204564,#204565,#204566,#204567,#204568,#204569,
#204570,#204571,#204572,#204573,#204574,#204575,#204576,#204577,#204578,
#204579,#204580,#204581,#204582,#204583,#204584,#204585,#204586,#204587,
#204588,#204589,#204590,#204591,#204592,#204593,#204594,#204595,#204596,
#204597,#204598,#204599,#204600,#204601,#204602,#204603,#204604,#204605,
#204606,#204607,#204608,#204609,#204610,#204611,#204612,#204613,#204614,
#204615,#204616),.UNSPECIFIED.,.F.,.F.,(4,3,3,3,3,3,3,3,3,3,3,3,3,3,3,3,
3,3,3,3,3,3,3,3,3,3,3,3,3,3,3,3,3,3,3,4),(171.305836600057,171.407491404046,
171.509232486424,171.611015128153,171.712976057781,171.799869393442,171.903390392073,
172.006760388742,172.110012049377,172.213200068173,172.316358267267,172.419520427281,
172.522790560255,172.626117812871,172.729627673424,172.798705843404,172.901009665115,
173.003159435031,173.105191801349,173.207161461353,173.309103780221,173.411054082656,
173.513126731748,173.615262377252,173.717603714352,173.797542293366,173.903815640338,
174.015386028212,174.121306049069,174.227126474861,174.332875046754,174.43857941621,
174.544296925171,174.650019520939,174.75581508523,174.796378743328),
 .UNSPECIFIED.);
#2062=B_SPLINE_CURVE_WITH_KNOTS('',3,(#204619,#204620,#204621,#204622,#204623,
#204624,#204625,#204626,#204627,#204628,#204629,#204630,#204631,#204632,
#204633,#204634,#204635,#204636,#204637,#204638,#204639,#204640,#204641,
#204642,#204643,#204644,#204645,#204646,#204647,#204648,#204649,#204650,
#204651,#204652,#204653,#204654,#204655,#204656,#204657,#204658,#204659,
#204660,#204661,#204662,#204663,#204664,#204665,#204666,#204667,#204668,
#204669,#204670,#204671,#204672,#204673,#204674,#204675,#204676,#204677,
#204678,#204679,#204680,#204681,#204682,#204683,#204684,#204685,#204686,
#204687,#204688,#204689,#204690,#204691,#204692,#204693,#204694,#204695,
#204696,#204697,#204698,#204699,#204700,#204701,#204702,#204703,#204704,
#204705,#204706,#204707,#204708,#204709,#204710,#204711,#204712,#204713,
#204714,#204715,#204716,#204717,#204718,#204719,#204720,#204721,#204722,
#204723,#204724,#204725,#204726,#204727,#204728,#204729,#204730,#204731,
#204732,#204733,#204734,#204735,#204736,#204737,#204738,#204739,#204740,
#204741,#204742,#204743,#204744,#204745,#204746,#204747,#204748,#204749,
#204750,#204751,#204752,#204753,#204754,#204755,#204756,#204757,#204758,
#204759,#204760,#204761,#204762,#204763,#204764,#204765,#204766,#204767,
#204768,#204769,#204770,#204771,#204772,#204773,#204774,#204775,#204776,
#204777,#204778),.UNSPECIFIED.,.F.,.F.,(4,3,3,3,3,3,3,3,3,3,3,3,3,3,3,3,
3,3,3,3,3,3,3,3,3,3,3,3,3,3,3,3,3,3,3,3,3,3,3,3,3,3,3,3,3,3,3,3,3,3,3,3,
3,4),(-172.787594226707,-172.684274547493,-172.581108276202,-172.478063417649,
-172.375083759813,-172.272135157488,-172.169183508487,-172.066127058214,
-171.963013611671,-171.859723903019,-171.799869393442,-171.696296383671,
-171.592873066918,-171.489566341367,-171.386322206412,-171.283106906827,
-171.179886727883,-171.076557515714,-170.973170499612,-170.8696003913,-170.80103294348,
-170.697770746273,-170.594663913509,-170.491680608289,-170.388763994098,
-170.285879836938,-170.182993947235,-170.08000156422,-169.976953319269,
-169.873721356035,-169.802196493519,-169.698775105051,-169.595507070885,
-169.492360335737,-169.38927900122,-169.286229069815,-169.183176587192,
-169.080017495714,-168.976802215422,-168.873404545781,-168.803360043557,
-168.699944492337,-168.59668192921,-168.493540087422,-168.390463287585,
-168.287417524489,-168.184368835746,-168.081212930417,-167.978000500935,
-167.874605105352,-167.804523593595,-167.699655977959,-167.594982656148,
-167.553337646663),.UNSPECIFIED.);
#2063=B_SPLINE_CURVE_WITH_KNOTS('',3,(#204781,#204782,#204783,#204784,#204785,
#204786,#204787,#204788,#204789,#204790,#204791,#204792,#204793,#204794,
#204795,#204796,#204797,#204798,#204799,#204800,#204801,#204802,#204803,
#204804,#204805,#204806,#204807,#204808,#204809,#204810,#204811,#204812,
#204813,#204814,#204815,#204816,#204817,#204818,#204819,#204820,#204821,
#204822,#204823,#204824,#204825,#204826,#204827,#204828,#204829,#204830,
#204831,#204832,#204833,#204834,#204835,#204836,#204837,#204838,#204839,
#204840,#204841,#204842,#204843,#204844,#204845,#204846,#204847,#204848,
#204849,#204850,#204851,#204852,#204853,#204854,#204855,#204856,#204857,
#204858,#204859,#204860,#204861,#204862,#204863,#204864,#204865,#204866,
#204867,#204868,#204869,#204870,#204871,#204872,#204873,#204874,#204875,
#204876,#204877,#204878,#204879,#204880,#204881,#204882,#204883,#204884,
#204885,#204886),.UNSPECIFIED.,.F.,.F.,(4,3,3,3,3,3,3,3,3,3,3,3,3,3,3,3,
3,3,3,3,3,3,3,3,3,3,3,3,3,3,3,3,3,3,3,4),(171.305836553012,171.407491357116,
171.509232440247,171.611015083074,171.712976014387,171.799869393442,171.903390296067,
172.006760196182,172.110011759924,172.213199681674,172.316357783713,172.419519846812,
172.522789883762,172.626117040711,172.729626807232,172.798705843404,172.901009858667,
173.003159822786,173.105192383572,173.207162238204,173.309104751679,173.411055248523,
173.513128090537,173.615263928529,173.717605455249,173.797542293366,173.90381549814,
174.015385903789,174.121305781442,174.227126064404,174.332874494259,174.438578722884,
174.544296093967,174.650018553652,174.755813985758,174.796378743328),
 .UNSPECIFIED.);
#2064=B_SPLINE_CURVE_WITH_KNOTS('',3,(#204889,#204890,#204891,#204892,#204893,
#204894,#204895,#204896,#204897,#204898,#204899,#204900,#204901,#204902,
#204903,#204904,#204905,#204906,#204907,#204908,#204909,#204910,#204911,
#204912,#204913,#204914,#204915,#204916,#204917,#204918,#204919,#204920,
#204921,#204922,#204923,#204924,#204925,#204926,#204927,#204928,#204929,
#204930,#204931,#204932,#204933,#204934,#204935,#204936,#204937,#204938,
#204939,#204940,#204941,#204942,#204943,#204944,#204945,#204946,#204947,
#204948,#204949,#204950,#204951,#204952,#204953,#204954,#204955,#204956,
#204957,#204958,#204959,#204960,#204961,#204962,#204963,#204964,#204965,
#204966,#204967,#204968,#204969,#204970,#204971,#204972,#204973,#204974,
#204975,#204976,#204977,#204978,#204979,#204980,#204981,#204982,#204983,
#204984,#204985,#204986,#204987,#204988,#204989,#204990,#204991,#204992,
#204993,#204994,#204995,#204996,#204997,#204998,#204999,#205000,#205001,
#205002,#205003,#205004,#205005,#205006,#205007,#205008,#205009,#205010,
#205011,#205012,#205013,#205014,#205015,#205016,#205017,#205018,#205019,
#205020,#205021,#205022,#205023,#205024,#205025,#205026,#205027,#205028,
#205029,#205030,#205031,#205032,#205033,#205034,#205035,#205036,#205037,
#205038,#205039,#205040,#205041,#205042,#205043,#205044,#205045,#205046,
#205047,#205048),.UNSPECIFIED.,.F.,.F.,(4,3,3,3,3,3,3,3,3,3,3,3,3,3,3,3,
3,3,3,3,3,3,3,3,3,3,3,3,3,3,3,3,3,3,3,3,3,3,3,3,3,3,3,3,3,3,3,3,3,3,3,3,
3,4),(-172.787594226732,-172.684274540723,-172.581108262565,-172.478063397069,
-172.375083732247,-172.272135122901,-172.169183466856,-172.06612700955,
-171.963013555969,-171.859723840347,-171.799869393442,-171.69629638248,
-171.592873064501,-171.489566337677,-171.386322201422,-171.28310690051,
-171.179886720216,-171.076557506667,-170.973170489168,-170.869600379445,
-170.801032943481,-170.697770749322,-170.594663919649,-170.491680617572,
-170.388764006554,-170.285879852593,-170.18299396611,-170.080001586328,
-169.976953344622,-169.873721384615,-169.802196493519,-169.69877510374,
-169.595507068251,-169.492360331767,-169.389278995906,-169.286229063151,
-169.183176579175,-169.080017486348,-168.976802204708,-168.873404533735,
-168.803360043557,-168.699944492016,-168.596681928558,-168.493540086429,
-168.390463286242,-168.28741752279,-168.184368833685,-168.081212927987,
-167.978000498131,-167.874605102172,-167.804523593595,-167.699655978575,
-167.594982657392,-167.553337655846),.UNSPECIFIED.);
#2065=B_SPLINE_CURVE_WITH_KNOTS('',3,(#205051,#205052,#205053,#205054,#205055,
#205056,#205057,#205058,#205059,#205060,#205061,#205062,#205063,#205064,
#205065,#205066,#205067,#205068,#205069,#205070,#205071,#205072,#205073,
#205074,#205075,#205076,#205077,#205078,#205079,#205080,#205081,#205082,
#205083,#205084,#205085,#205086,#205087,#205088,#205089,#205090,#205091,
#205092,#205093,#205094,#205095,#205096,#205097,#205098,#205099,#205100,
#205101,#205102,#205103,#205104,#205105,#205106,#205107,#205108,#205109,
#205110,#205111,#205112,#205113,#205114,#205115,#205116,#205117,#205118,
#205119,#205120,#205121,#205122,#205123,#205124,#205125,#205126,#205127,
#205128,#205129,#205130,#205131,#205132,#205133,#205134,#205135,#205136,
#205137,#205138,#205139,#205140,#205141,#205142,#205143,#205144,#205145,
#205146,#205147,#205148,#205149,#205150,#205151,#205152,#205153,#205154,
#205155,#205156),.UNSPECIFIED.,.F.,.F.,(4,3,3,3,3,3,3,3,3,3,3,3,3,3,3,3,
3,3,3,3,3,3,3,3,3,3,3,3,3,3,3,3,3,3,3,4),(171.305836564222,171.407491368278,
171.509232451096,171.611015093464,171.71297602408,171.799869393442,171.903390335715,
172.006760275705,172.110011879462,172.21319984129,172.31635798341,172.419520086533,
172.522790163139,172.626117359596,172.72962716495,172.798705843404,172.901009778732,
173.003159662647,173.105192143119,173.207161917372,173.309104350476,173.411054767032,
173.513127529371,173.615263287867,173.717604736276,173.797542293366,173.903815556868,
174.015385955175,174.121305891971,174.227126233922,174.332874722438,174.438579009226,
174.544296437251,174.650018953138,174.755814439837,174.796378743328),
 .UNSPECIFIED.);
#2066=B_SPLINE_CURVE_WITH_KNOTS('',3,(#205159,#205160,#205161,#205162,#205163,
#205164,#205165,#205166,#205167,#205168,#205169,#205170,#205171,#205172,
#205173,#205174,#205175,#205176,#205177,#205178,#205179,#205180,#205181,
#205182,#205183,#205184,#205185,#205186,#205187,#205188,#205189,#205190,
#205191,#205192,#205193,#205194,#205195,#205196,#205197,#205198,#205199,
#205200,#205201,#205202,#205203,#205204,#205205,#205206,#205207,#205208,
#205209,#205210,#205211,#205212,#205213,#205214,#205215,#205216,#205217,
#205218,#205219,#205220,#205221,#205222,#205223,#205224,#205225,#205226,
#205227,#205228,#205229,#205230,#205231,#205232,#205233,#205234,#205235,
#205236,#205237,#205238,#205239,#205240,#205241,#205242,#205243,#205244,
#205245,#205246,#205247,#205248,#205249,#205250,#205251,#205252,#205253,
#205254,#205255,#205256,#205257,#205258,#205259,#205260,#205261,#205262,
#205263,#205264,#205265,#205266,#205267,#205268,#205269,#205270,#205271,
#205272,#205273,#205274,#205275,#205276,#205277,#205278,#205279,#205280,
#205281,#205282,#205283,#205284,#205285,#205286,#205287,#205288,#205289,
#205290,#205291,#205292,#205293,#205294,#205295,#205296,#205297,#205298,
#205299,#205300,#205301,#205302,#205303,#205304,#205305,#205306,#205307,
#205308,#205309,#205310,#205311,#205312,#205313,#205314,#205315,#205316,
#205317,#205318),.UNSPECIFIED.,.F.,.F.,(4,3,3,3,3,3,3,3,3,3,3,3,3,3,3,3,
3,3,3,3,3,3,3,3,3,3,3,3,3,3,3,3,3,3,3,3,3,3,3,3,3,3,3,3,3,3,3,3,3,3,3,3,
3,4),(-172.787594226351,-172.684274645609,-172.581108473843,-172.478063715916,
-172.375084159336,-172.272135658752,-172.169184111836,-172.066127763492,
-171.963014418944,-171.859724811317,-171.799869393442,-171.696296400939,
-171.592873101958,-171.489566394852,-171.386322278747,-171.283106998388,
-171.179886839023,-171.076557646842,-170.973170650988,-170.869600563122,
-170.801032943481,-170.69777070211,-170.594663824546,-170.491680473781,
-170.388763813606,-170.285879610087,-170.182993673711,-170.080001243854,
-169.976952951891,-169.873720941887,-169.802196493519,-169.698775124036,
-169.595507109046,-169.492360393262,-169.389279078215,-169.286229166357,
-169.183176703332,-169.080017631391,-168.976802370632,-168.873404720303,
-168.803360043557,-168.699944496997,-168.59668193866,-168.493540101833,
-168.39046330706,-168.287417549124,-168.184368865631,-168.081212965654,
-167.978000541589,-167.874605151471,-167.804523593595,-167.699655968957,
-167.594982637949,-167.55333773927),.UNSPECIFIED.);
#2067=B_SPLINE_CURVE_WITH_KNOTS('',3,(#205321,#205322,#205323,#205324,#205325,
#205326,#205327,#205328,#205329,#205330,#205331,#205332,#205333,#205334,
#205335,#205336,#205337,#205338,#205339,#205340,#205341,#205342,#205343,
#205344,#205345,#205346,#205347,#205348,#205349,#205350,#205351,#205352,
#205353,#205354,#205355,#205356,#205357,#205358,#205359,#205360,#205361,
#205362,#205363,#205364,#205365,#205366,#205367,#205368,#205369,#205370,
#205371,#205372,#205373,#205374,#205375,#205376,#205377,#205378,#205379,
#205380,#205381,#205382,#205383,#205384,#205385,#205386,#205387,#205388,
#205389,#205390,#205391,#205392,#205393,#205394,#205395,#205396,#205397,
#205398,#205399,#205400,#205401,#205402,#205403,#205404,#205405,#205406,
#205407,#205408,#205409,#205410,#205411,#205412,#205413,#205414,#205415,
#205416,#205417,#205418,#205419,#205420,#205421,#205422,#205423,#205424,
#205425,#205426),.UNSPECIFIED.,.F.,.F.,(4,3,3,3,3,3,3,3,3,3,3,3,3,3,3,3,
3,3,3,3,3,3,3,3,3,3,3,3,3,3,3,3,3,3,3,4),(171.305836655045,171.407491458764,
171.509232539317,171.611015178365,171.712976103912,171.799869393442,171.903390623982,
172.006760853885,172.110012748576,172.2132010018,172.316359435341,172.419521829469,
172.522792194405,172.626119678124,172.729629765827,172.798705843404,172.90100919765,
173.00315849853,173.10519039517,173.207159585109,173.309101433958,173.411051266852,
173.513123449993,173.615258630591,173.71759950971,173.797542293366,173.903815983742,
174.01538632869,174.121306695383,174.227127466107,174.332876381024,174.438581090584,
174.544298932523,174.650021856933,174.755817740451,174.796378743328),
 .UNSPECIFIED.);
#2068=B_SPLINE_CURVE_WITH_KNOTS('',3,(#205429,#205430,#205431,#205432,#205433,
#205434,#205435,#205436,#205437,#205438,#205439,#205440,#205441,#205442,
#205443,#205444),.UNSPECIFIED.,.F.,.F.,(4,2,2,2,2,2,2,4),(-3.36796842350093,
-3.29693348725048,-3.2276059680982,-3.10443413185248,-3.02217223145102,
-2.85176927650461,-2.77989380916357,-2.68789745416103),.UNSPECIFIED.);
#2069=B_SPLINE_CURVE_WITH_KNOTS('',3,(#205448,#205449,#205450,#205451,#205452,
#205453,#205454,#205455,#205456,#205457,#205458,#205459,#205460,#205461,
#205462),.UNSPECIFIED.,.F.,.F.,(4,1,1,1,1,1,1,1,1,1,1,1,4),(2.02178176728025,
2.43673748880502,2.92408498656602,3.41143248432702,3.89877998208802,4.38612747984902,
4.87347497761003,5.36082247537103,5.84816997313203,6.33551747089303,6.82286496865404,
7.31021246641504,7.59153924858055),.UNSPECIFIED.);
#2070=B_SPLINE_CURVE_WITH_KNOTS('',3,(#205465,#205466,#205467,#205468,#205469,
#205470,#205471,#205472,#205473,#205474,#205475,#205476,#205477,#205478,
#205479,#205480,#205481,#205482,#205483,#205484,#205485,#205486,#205487,
#205488,#205489,#205490,#205491,#205492,#205493,#205494,#205495,#205496,
#205497,#205498),.UNSPECIFIED.,.F.,.F.,(4,2,2,2,2,2,2,2,2,2,2,2,2,2,2,2,
4),(2.08269173712794E-5,0.0904906817544001,0.176689485912824,0.297418593220784,
0.379377464742978,0.549734405369124,0.620055052536581,0.741861277008205,
0.810969949261042,0.891261322378703,1.03196791749396,1.11156489827869,1.23025736979253,
1.31034234680985,1.4491620241015,1.58466358484633,1.64869401953039),
 .UNSPECIFIED.);
#2071=B_SPLINE_CURVE_WITH_KNOTS('',3,(#205501,#205502,#205503,#205504,#205505,
#205506,#205507),.UNSPECIFIED.,.F.,.F.,(4,1,1,1,4),(183.127688252684,183.201986895449,
184.200823345411,185.199659795373,185.353966561798),.UNSPECIFIED.);
#2072=B_SPLINE_CURVE_WITH_KNOTS('',3,(#205509,#205510,#205511,#205512,#205513,
#205514,#205515,#205516,#205517,#205518,#205519,#205520,#205521,#205522,
#205523,#205524,#205525,#205526,#205527,#205528,#205529,#205530,#205531,
#205532,#205533,#205534,#205535,#205536,#205537,#205538,#205539,#205540,
#205541,#205542,#205543,#205544,#205545,#205546,#205547,#205548,#205549,
#205550,#205551,#205552,#205553,#205554,#205555,#205556,#205557,#205558,
#205559,#205560,#205561,#205562,#205563,#205564,#205565,#205566),
 .UNSPECIFIED.,.F.,.F.,(4,3,3,3,3,3,3,3,3,3,3,3,3,3,3,3,3,3,3,4),(185.353966561798,
185.451129862355,185.548173545581,185.645152144533,185.742096651447,185.839038013602,
185.93606867674,186.033145889087,186.130383557083,186.198496245335,186.297012011071,
186.39538977669,186.494243904503,186.592449804335,186.690624726039,186.788798244729,
186.888154383345,186.9864710254,187.086346912297,187.186222799194),
 .UNSPECIFIED.);
#2073=B_SPLINE_CURVE_WITH_KNOTS('',3,(#205570,#205571,#205572,#205573,#205574),
 .UNSPECIFIED.,.F.,.F.,(4,1,4),(185.353966561798,185.664466527893,186.663302977854),
 .UNSPECIFIED.);
#2074=B_SPLINE_CURVE_WITH_KNOTS('',3,(#205575,#205576,#205577,#205578,#205579,
#205580),.UNSPECIFIED.,.F.,.F.,(4,1,1,4),(183.128402505335,183.666793627969,
184.665630077931,185.353966561798),.UNSPECIFIED.);
#2075=B_SPLINE_CURVE_WITH_KNOTS('',3,(#205583,#205584,#205585,#205586,#205587,
#205588,#205589),.UNSPECIFIED.,.F.,.F.,(4,1,1,1,4),(183.127688302604,183.201986895449,
184.200823345411,185.199659795373,185.353966561798),.UNSPECIFIED.);
#2076=B_SPLINE_CURVE_WITH_KNOTS('',3,(#205591,#205592,#205593,#205594,#205595,
#205596,#205597,#205598,#205599,#205600,#205601,#205602,#205603,#205604,
#205605,#205606,#205607,#205608,#205609,#205610,#205611,#205612,#205613,
#205614,#205615,#205616,#205617,#205618,#205619,#205620,#205621,#205622,
#205623,#205624,#205625,#205626,#205627,#205628,#205629,#205630,#205631,
#205632,#205633,#205634,#205635,#205636,#205637,#205638,#205639,#205640,
#205641,#205642,#205643,#205644,#205645,#205646,#205647,#205648),
 .UNSPECIFIED.,.F.,.F.,(4,3,3,3,3,3,3,3,3,3,3,3,3,3,3,3,3,3,3,4),(185.353966561798,
185.451129857721,185.548173538225,185.645152135629,185.742096642157,185.839038005082,
185.936068670734,186.033145886574,186.130383559583,186.198496245335,186.297011743078,
186.39538923924,186.494243434233,186.592449062934,186.690623713446,186.78879696123,
186.88815342072,186.986469795236,187.086346297213,187.186222799189),
 .UNSPECIFIED.);
#2077=B_SPLINE_CURVE_WITH_KNOTS('',3,(#205652,#205653,#205654,#205655,#205656),
 .UNSPECIFIED.,.F.,.F.,(4,1,4),(185.353966561798,185.664466527893,186.663302977854),
 .UNSPECIFIED.);
#2078=B_SPLINE_CURVE_WITH_KNOTS('',3,(#205657,#205658,#205659,#205660,#205661,
#205662),.UNSPECIFIED.,.F.,.F.,(4,1,1,4),(183.128402568106,183.666793627969,
184.665630077931,185.353966561798),.UNSPECIFIED.);
#2079=B_SPLINE_CURVE_WITH_KNOTS('',3,(#205665,#205666,#205667,#205668,#205669,
#205670,#205671),.UNSPECIFIED.,.F.,.F.,(4,1,1,1,4),(183.127688309466,183.201986895449,
184.200823345411,185.199659795373,185.353966561798),.UNSPECIFIED.);
#2080=B_SPLINE_CURVE_WITH_KNOTS('',3,(#205673,#205674,#205675,#205676,#205677,
#205678,#205679,#205680,#205681,#205682,#205683,#205684,#205685,#205686,
#205687,#205688,#205689,#205690,#205691,#205692,#205693,#205694,#205695,
#205696,#205697,#205698,#205699,#205700,#205701,#205702,#205703,#205704,
#205705,#205706,#205707,#205708,#205709,#205710,#205711,#205712,#205713,
#205714,#205715,#205716,#205717,#205718,#205719,#205720,#205721,#205722,
#205723,#205724,#205725,#205726,#205727,#205728,#205729,#205730),
 .UNSPECIFIED.,.F.,.F.,(4,3,3,3,3,3,3,3,3,3,3,3,3,3,3,3,3,3,3,4),(185.353966561798,
185.451129857085,185.548173537216,185.645152134409,185.742096640885,185.839038003917,
185.936068669915,186.033145886238,186.130383559937,186.198496245335,186.297011706217,
186.395389165318,186.494243369552,186.592448960961,186.690623574174,186.788796784698,
186.888153288321,186.986469626041,187.086346212615,187.186222799188),
 .UNSPECIFIED.);
#2081=B_SPLINE_CURVE_WITH_KNOTS('',3,(#205734,#205735,#205736,#205737,#205738),
 .UNSPECIFIED.,.F.,.F.,(4,1,4),(185.353966561798,185.664466527893,186.663302977854),
 .UNSPECIFIED.);
#2082=B_SPLINE_CURVE_WITH_KNOTS('',3,(#205739,#205740,#205741,#205742,#205743,
#205744),.UNSPECIFIED.,.F.,.F.,(4,1,1,4),(183.128402575235,183.666793627969,
184.665630077931,185.353966561798),.UNSPECIFIED.);
#2083=B_SPLINE_CURVE_WITH_KNOTS('',3,(#205747,#205748,#205749,#205750,#205751,
#205752,#205753),.UNSPECIFIED.,.F.,.F.,(4,1,1,1,4),(183.12768829285,183.201986895449,
184.200823345411,185.199659795373,185.353966561798),.UNSPECIFIED.);
#2084=B_SPLINE_CURVE_WITH_KNOTS('',3,(#205755,#205756,#205757,#205758,#205759,
#205760,#205761,#205762,#205763,#205764,#205765,#205766,#205767,#205768,
#205769,#205770,#205771,#205772,#205773,#205774,#205775,#205776,#205777,
#205778,#205779,#205780,#205781,#205782,#205783,#205784,#205785,#205786,
#205787,#205788,#205789,#205790,#205791,#205792,#205793,#205794,#205795,
#205796,#205797,#205798,#205799,#205800,#205801,#205802,#205803,#205804,
#205805,#205806,#205807,#205808,#205809,#205810,#205811,#205812),
 .UNSPECIFIED.,.F.,.F.,(4,3,3,3,3,3,3,3,3,3,3,3,3,3,3,3,3,3,3,4),(185.353966561798,
185.451129858625,185.54817353966,185.645152137366,185.742096643968,185.839038006741,
185.9360686719,186.033145887057,186.130383559085,186.198496245335,186.297011795472,
186.395389344314,186.494243526173,186.592449207881,186.690623911412,186.788797212158,
186.888153608916,186.986470035736,187.086346417463,187.18622279919),
 .UNSPECIFIED.);
#2085=B_SPLINE_CURVE_WITH_KNOTS('',3,(#205816,#205817,#205818,#205819,#205820),
 .UNSPECIFIED.,.F.,.F.,(4,1,4),(185.353966561798,185.664466527893,186.663302977854),
 .UNSPECIFIED.);
#2086=B_SPLINE_CURVE_WITH_KNOTS('',3,(#205821,#205822,#205823,#205824,#205825,
#205826),.UNSPECIFIED.,.F.,.F.,(4,1,1,4),(183.128402534571,183.666793627969,
184.665630077931,185.353966561798),.UNSPECIFIED.);
#2087=B_SPLINE_CURVE_WITH_KNOTS('',3,(#205829,#205830,#205831,#205832,#205833,
#205834),.UNSPECIFIED.,.F.,.F.,(4,1,1,4),(33.4844854751707,33.8935092369881,
34.3808567347491,34.5575191593334),.UNSPECIFIED.);
#2088=B_SPLINE_CURVE_WITH_KNOTS('',3,(#205836,#205837,#205838,#205839,#205840,
#205841,#205842,#205843,#205844,#205845,#205846,#205847,#205848,#205849,
#205850,#205851,#205852,#205853,#205854,#205855,#205856,#205857,#205858,
#205859,#205860,#205861,#205862,#205863,#205864,#205865,#205866,#205867,
#205868,#205869,#205870,#205871,#205872,#205873,#205874,#205875,#205876,
#205877,#205878,#205879,#205880,#205881,#205882,#205883,#205884,#205885,
#205886,#205887,#205888,#205889,#205890,#205891,#205892,#205893,#205894,
#205895,#205896,#205897,#205898,#205899,#205900,#205901,#205902,#205903,
#205904,#205905,#205906,#205907,#205908,#205909,#205910,#205911,#205912,
#205913,#205914,#205915,#205916,#205917,#205918,#205919,#205920,#205921,
#205922,#205923,#205924,#205925,#205926,#205927,#205928,#205929,#205930,
#205931,#205932,#205933,#205934,#205935,#205936,#205937,#205938,#205939,
#205940,#205941,#205942,#205943,#205944,#205945,#205946,#205947,#205948,
#205949,#205950,#205951,#205952,#205953,#205954,#205955,#205956,#205957,
#205958,#205959,#205960,#205961,#205962,#205963,#205964,#205965,#205966,
#205967,#205968,#205969,#205970,#205971,#205972,#205973,#205974,#205975,
#205976,#205977,#205978,#205979,#205980,#205981,#205982,#205983,#205984,
#205985,#205986,#205987,#205988,#205989),.UNSPECIFIED.,.F.,.F.,(4,3,3,3,
3,3,3,3,3,3,3,3,3,3,3,3,3,3,3,3,3,3,3,3,3,3,3,3,3,3,3,3,3,3,3,3,3,3,3,3,
3,3,3,3,3,3,3,3,3,3,3,4),(34.5575191894877,34.6447569868975,34.7319919193617,
34.8192474749927,34.8682042325101,34.9553345482705,35.0424483237626,35.1295651730742,
35.2166773096183,35.3038088155763,35.3555517302711,35.4426813818879,35.5297944898996,
35.6169106732714,35.7040221463605,35.7911529985374,35.8428992280321,35.9300290900273,
36.0171424031941,36.1042587818684,36.1913704442032,36.2785014746032,36.3302467257931,
36.4173754321069,36.5044875913759,36.5916028300414,36.6787133629673,36.7658432901786,
36.8175942235541,36.9047259024205,36.9918410382111,37.0789592304618,37.1660726969111,
37.2532055011073,37.3049417213151,37.3920685401476,37.4791788111556,37.5662921786384,
37.6534008545103,37.7405289626034,37.7922892190761,37.8794201719593,37.966534565058,
38.0536519969681,38.1407646949544,38.2278967250119,38.2796367168371,38.3664398085489,
38.4532349861649,38.5400191597449,38.6268188966943,38.6945925143091),
 .UNSPECIFIED.);
#2089=B_SPLINE_CURVE_WITH_KNOTS('',3,(#205993,#205994,#205995,#205996,#205997,
#205998,#205999,#206000,#206001,#206002,#206003),.UNSPECIFIED.,.F.,.F.,
(4,1,1,1,1,1,1,1,4),(34.5575192147677,34.7582752591941,35.2456227569552,
35.7329702547162,36.2203177524772,36.7076652502382,37.1950127479992,37.6823602457602,
38.1697077435212),.UNSPECIFIED.);
#2090=B_SPLINE_CURVE_WITH_KNOTS('',3,(#206004,#206005,#206006,#206007,#206008,
#206009,#206010,#206011,#206012,#206013,#206014,#206015,#206016,#206017,
#206018,#206019,#206020,#206021,#206022,#206023,#206024,#206025,#206026,
#206027,#206028,#206029,#206030,#206031,#206032,#206033,#206034,#206035,
#206036,#206037,#206038,#206039,#206040,#206041,#206042,#206043,#206044,
#206045,#206046),.UNSPECIFIED.,.F.,.F.,(4,3,3,3,3,3,3,3,3,3,3,3,3,3,4),
(33.4844725988534,33.5715877001674,33.6586993242475,33.7458293437006,33.7835802636721,
33.8707089685104,33.9578211263055,34.0449363635138,34.1320468949955,34.2191768207952,
34.2709277614331,34.3584567371214,34.4459664694995,34.5334668195807,34.5575191894877),
 .UNSPECIFIED.);
#2091=B_SPLINE_CURVE_WITH_KNOTS('',3,(#206049,#206050,#206051,#206052,#206053,
#206054),.UNSPECIFIED.,.F.,.F.,(4,1,1,4),(33.4844854782753,33.8935092369881,
34.3808567347491,34.5575191593289),.UNSPECIFIED.);
#2092=B_SPLINE_CURVE_WITH_KNOTS('',3,(#206056,#206057,#206058,#206059,#206060,
#206061,#206062,#206063,#206064,#206065,#206066,#206067,#206068,#206069,
#206070,#206071,#206072,#206073,#206074,#206075,#206076,#206077,#206078,
#206079,#206080,#206081,#206082,#206083,#206084,#206085,#206086,#206087,
#206088,#206089,#206090,#206091,#206092,#206093,#206094,#206095,#206096,
#206097,#206098,#206099,#206100,#206101,#206102,#206103,#206104,#206105,
#206106,#206107,#206108,#206109,#206110,#206111,#206112,#206113,#206114,
#206115,#206116,#206117,#206118,#206119,#206120,#206121,#206122,#206123,
#206124,#206125,#206126,#206127,#206128,#206129,#206130,#206131,#206132,
#206133,#206134,#206135,#206136,#206137,#206138,#206139,#206140,#206141,
#206142,#206143,#206144,#206145,#206146,#206147,#206148,#206149,#206150,
#206151,#206152,#206153,#206154,#206155,#206156,#206157,#206158,#206159,
#206160,#206161,#206162,#206163,#206164,#206165,#206166,#206167,#206168,
#206169,#206170,#206171,#206172,#206173,#206174,#206175,#206176,#206177,
#206178,#206179,#206180,#206181,#206182,#206183,#206184,#206185,#206186,
#206187,#206188,#206189,#206190,#206191,#206192,#206193,#206194,#206195,
#206196,#206197,#206198,#206199,#206200,#206201,#206202,#206203,#206204,
#206205,#206206,#206207,#206208,#206209),.UNSPECIFIED.,.F.,.F.,(4,3,3,3,
3,3,3,3,3,3,3,3,3,3,3,3,3,3,3,3,3,3,3,3,3,3,3,3,3,3,3,3,3,3,3,3,3,3,3,3,
3,3,3,3,3,3,3,3,3,3,3,4),(34.5575191894877,34.6447569757657,34.7319918970944,
34.8192474416769,34.8682042325101,34.9553345524685,35.0424483321962,35.1295651857588,
35.2166773265522,35.3038088367198,35.3555517302711,35.4426813814716,35.5297944890805,
35.6169106720737,35.7040221447989,35.7911529966377,35.8428992280321,35.9300290910938,
36.0171424053112,36.1042587850018,36.191370448331,36.278501479683,36.3302467257931,
36.4173754284676,36.5044875841013,36.5916028191727,36.6787133485363,36.7658432722657,
36.8175942235541,36.9047259080441,36.9918410494598,37.0789592472834,37.1660727192629,
37.2532055288754,37.3049417213151,37.3920685377782,37.4791788064371,37.5662921716237,
37.6534008452347,37.7405289511405,37.7922892190762,37.8794201571563,37.966534535352,
38.0536519523545,38.1407646354665,38.2278966508317,38.2796367168372,38.3664398614179,
38.4532350920939,38.5400193187296,38.6268191082651,38.6945925143091),
 .UNSPECIFIED.);
#2093=B_SPLINE_CURVE_WITH_KNOTS('',3,(#206213,#206214,#206215,#206216,#206217,
#206218,#206219,#206220,#206221,#206222,#206223),.UNSPECIFIED.,.F.,.F.,
(4,1,1,1,1,1,1,1,4),(34.5575192147699,34.7582752591942,35.2456227569552,
35.7329702547162,36.2203177524772,36.7076652502382,37.1950127479992,37.6823602457602,
38.1697077435212),.UNSPECIFIED.);
#2094=B_SPLINE_CURVE_WITH_KNOTS('',3,(#206224,#206225,#206226,#206227,#206228,
#206229,#206230,#206231,#206232,#206233,#206234,#206235,#206236,#206237,
#206238,#206239,#206240,#206241,#206242,#206243,#206244,#206245,#206246,
#206247,#206248,#206249,#206250,#206251,#206252,#206253,#206254,#206255,
#206256,#206257,#206258,#206259,#206260,#206261,#206262,#206263,#206264,
#206265,#206266),.UNSPECIFIED.,.F.,.F.,(4,3,3,3,3,3,3,3,3,3,3,3,3,3,4),
(33.4844725969432,33.5715876990605,33.6586993239259,33.7458293441317,33.7835802636722,
33.8707089656242,33.9578211205362,34.0449363548941,34.1320468835505,34.2191768065887,
34.2709277614332,34.3584567439305,34.4459664831206,34.5334668399684,34.5575191894877),
 .UNSPECIFIED.);
#2095=B_SPLINE_CURVE_WITH_KNOTS('',3,(#206401,#206402,#206403,#206404,#206405,
#206406,#206407,#206408,#206409,#206410,#206411,#206412,#206413,#206414,
#206415,#206416,#206417,#206418,#206419,#206420,#206421,#206422,#206423,
#206424,#206425,#206426,#206427,#206428,#206429,#206430,#206431,#206432,
#206433,#206434,#206435,#206436,#206437,#206438,#206439,#206440,#206441,
#206442,#206443,#206444,#206445,#206446,#206447,#206448,#206449,#206450,
#206451,#206452,#206453,#206454,#206455,#206456,#206457,#206458,#206459,
#206460,#206461,#206462,#206463,#206464,#206465,#206466,#206467,#206468,
#206469,#206470,#206471,#206472,#206473,#206474,#206475,#206476,#206477,
#206478,#206479,#206480,#206481,#206482,#206483,#206484,#206485,#206486,
#206487,#206488),.UNSPECIFIED.,.F.,.F.,(4,3,3,3,3,3,3,3,3,3,3,3,3,3,3,3,
3,3,3,3,3,3,3,3,3,3,3,3,3,4),(0.,0.0223800438562092,0.0455571551208265,
0.0675550647019532,0.0773342777042101,0.0821512753707187,0.0865889152558688,
0.110577888018852,0.135008177242286,0.157206748761003,0.165672870216831,
0.170323072593406,0.173915834948667,0.198993095015584,0.224022472738064,
0.248522734273475,0.258554636060882,0.264135020452961,0.288903377496841,
0.314991214965925,0.34107905243501,0.351267090483404,0.355315312120404,
0.381664714548268,0.403487578295303,0.410694478291004,0.416463279199868,
0.443066534667853,0.469275862304387,0.472065636590528),.UNSPECIFIED.);
#2096=B_SPLINE_CURVE_WITH_KNOTS('',3,(#206489,#206490,#206491,#206492,#206493,
#206494,#206495,#206496,#206497,#206498,#206499,#206500,#206501,#206502,
#206503,#206504,#206505,#206506,#206507,#206508,#206509,#206510,#206511,
#206512,#206513,#206514,#206515,#206516,#206517,#206518,#206519,#206520,
#206521,#206522,#206523,#206524,#206525,#206526,#206527,#206528,#206529,
#206530,#206531,#206532,#206533,#206534,#206535,#206536,#206537,#206538,
#206539,#206540,#206541,#206542,#206543,#206544,#206545,#206546,#206547,
#206548,#206549,#206550,#206551,#206552,#206553,#206554,#206555,#206556,
#206557,#206558,#206559,#206560,#206561,#206562,#206563,#206564,#206565,
#206566,#206567,#206568,#206569,#206570,#206571,#206572,#206573,#206574,
#206575,#206576),.UNSPECIFIED.,.F.,.F.,(4,3,3,3,3,3,3,3,3,3,3,3,3,3,3,3,
3,3,3,3,3,3,3,3,3,3,3,3,3,4),(0.,0.0260517790363247,0.0527225331749561,
0.0776790837678674,0.0889727987852075,0.0959464344588869,0.100845925000849,
0.126855201330774,0.152534130317405,0.176212520341607,0.186122361847472,
0.192547946339425,0.196620306261614,0.221672219573634,0.246724132885653,
0.272050620367204,0.282513655994357,0.286631738476199,0.311154772354938,
0.335765994613648,0.360166888444423,0.370324933502905,0.375577979330509,
0.39932663886447,0.417608625696714,0.42311115157445,0.427811305959952,0.450556505121144,
0.47164802816755,0.474022601254833),.UNSPECIFIED.);
#2097=B_SPLINE_CURVE_WITH_KNOTS('',3,(#206577,#206578,#206579,#206580,#206581,
#206582,#206583,#206584,#206585,#206586,#206587,#206588,#206589,#206590,
#206591,#206592,#206593,#206594,#206595,#206596,#206597,#206598,#206599,
#206600,#206601,#206602,#206603,#206604,#206605,#206606,#206607,#206608,
#206609,#206610,#206611,#206612,#206613,#206614,#206615,#206616,#206617,
#206618,#206619,#206620,#206621,#206622,#206623,#206624,#206625,#206626,
#206627,#206628,#206629,#206630,#206631,#206632,#206633,#206634,#206635,
#206636,#206637,#206638,#206639,#206640,#206641,#206642,#206643,#206644,
#206645,#206646,#206647,#206648,#206649,#206650,#206651,#206652,#206653,
#206654,#206655,#206656,#206657,#206658,#206659,#206660,#206661,#206662,
#206663,#206664),.UNSPECIFIED.,.F.,.F.,(4,3,3,3,3,3,3,3,3,3,3,3,3,3,3,3,
3,3,3,3,3,3,3,3,3,3,3,3,3,4),(0.,0.0223800372151332,0.0455571433122737,
0.0675550536686484,0.0773342673604862,0.0821512524289193,0.0865889078224679,
0.110577875996286,0.135008164711438,0.157206738276085,0.165672856963219,
0.170323012283074,0.173915733667268,0.198992994974291,0.224022472738052,
0.248477225379953,0.258554635842646,0.264135020504929,0.288903381765905,
0.314991218209838,0.341079054653772,0.351267092682162,0.355315313446979,
0.381664716363141,0.403487580067799,0.410694485847216,0.41646327764549,
0.443066533245083,0.469275862304372,0.472065636984178),.UNSPECIFIED.);
#2098=B_SPLINE_CURVE_WITH_KNOTS('',3,(#206665,#206666,#206667,#206668,#206669,
#206670,#206671,#206672,#206673,#206674,#206675,#206676,#206677,#206678,
#206679,#206680,#206681,#206682,#206683,#206684,#206685,#206686,#206687,
#206688,#206689,#206690,#206691,#206692,#206693,#206694,#206695,#206696,
#206697,#206698,#206699,#206700,#206701,#206702,#206703,#206704,#206705,
#206706,#206707,#206708,#206709,#206710,#206711,#206712,#206713,#206714,
#206715,#206716,#206717,#206718,#206719,#206720,#206721,#206722,#206723,
#206724,#206725,#206726,#206727,#206728,#206729,#206730,#206731,#206732,
#206733,#206734,#206735,#206736,#206737,#206738,#206739,#206740,#206741,
#206742,#206743,#206744,#206745,#206746,#206747,#206748,#206749,#206750,
#206751,#206752),.UNSPECIFIED.,.F.,.F.,(4,3,3,3,3,3,3,3,3,3,3,3,3,3,3,3,
3,3,3,3,3,3,3,3,3,3,3,3,3,4),(0.,0.0260517968486712,0.0527225544316126,
0.0776790985121134,0.088972803707389,0.0959464341599202,0.100845925569268,
0.126855201703201,0.152534124099972,0.176212516457141,0.186122361672799,
0.192547951517572,0.196620308043645,0.221672220464654,0.246724132885662,
0.272050621021719,0.282513655344617,0.286631737801889,0.311154771378497,
0.335765992439757,0.360166881962943,0.370324927588301,0.375577975882316,
0.399326629362452,0.417608623757103,0.423111147264353,0.427811294162416,
0.450556481123398,0.471648028167544,0.474022601254839),.UNSPECIFIED.);
#2099=B_SPLINE_CURVE_WITH_KNOTS('',3,(#206753,#206754,#206755,#206756,#206757,
#206758,#206759,#206760,#206761,#206762,#206763,#206764,#206765,#206766,
#206767,#206768,#206769,#206770,#206771,#206772,#206773,#206774,#206775,
#206776,#206777,#206778,#206779,#206780,#206781,#206782,#206783,#206784,
#206785,#206786,#206787,#206788,#206789,#206790,#206791,#206792,#206793,
#206794,#206795,#206796,#206797,#206798,#206799,#206800,#206801,#206802,
#206803,#206804,#206805,#206806,#206807,#206808,#206809,#206810,#206811,
#206812,#206813,#206814,#206815,#206816,#206817,#206818,#206819,#206820,
#206821,#206822,#206823,#206824,#206825,#206826,#206827,#206828,#206829,
#206830,#206831,#206832,#206833,#206834,#206835,#206836,#206837,#206838,
#206839,#206840),.UNSPECIFIED.,.F.,.F.,(4,3,3,3,3,3,3,3,3,3,3,3,3,3,3,3,
3,3,3,3,3,3,3,3,3,3,3,3,3,4),(0.,0.0226012852117639,0.0452025704235279,
0.067555058212843,0.0773342716206684,0.0821512618789957,0.0865889109720383,
0.110761871811172,0.134934832650306,0.157206742672241,0.165672862519276,
0.17032303759631,0.173915776335193,0.198993037124029,0.224022472738049,
0.24847722404691,0.258554635931002,0.264135020402494,0.289777625640233,
0.315428339653183,0.341079053666132,0.351267091758101,0.355315312641973,
0.381664715351708,0.403487579124147,0.410694481959163,0.416463278906866,
0.443066534477174,0.469275862304408,0.472065636821688),.UNSPECIFIED.);
#2100=B_SPLINE_CURVE_WITH_KNOTS('',3,(#206841,#206842,#206843,#206844,#206845,
#206846,#206847,#206848,#206849,#206850,#206851,#206852,#206853,#206854,
#206855,#206856,#206857,#206858,#206859,#206860,#206861,#206862,#206863,
#206864,#206865,#206866,#206867,#206868,#206869,#206870,#206871,#206872,
#206873,#206874,#206875,#206876,#206877,#206878,#206879,#206880,#206881,
#206882,#206883,#206884,#206885,#206886,#206887,#206888,#206889,#206890,
#206891,#206892,#206893,#206894,#206895,#206896,#206897,#206898,#206899,
#206900,#206901,#206902,#206903,#206904,#206905,#206906,#206907,#206908,
#206909,#206910,#206911,#206912,#206913,#206914,#206915,#206916,#206917,
#206918,#206919,#206920,#206921,#206922,#206923,#206924,#206925,#206926,
#206927,#206928),.UNSPECIFIED.,.F.,.F.,(4,3,3,3,3,3,3,3,3,3,3,3,3,3,3,3,
3,3,3,3,3,3,3,3,3,3,3,3,3,4),(0.,0.0259306190073998,0.0526009583628542,
0.0776790988226147,0.0889728038113335,0.0959464341623167,0.100845925575729,
0.126856858203815,0.152713971416374,0.177949842661688,0.186122361669415,
0.192547951595364,0.196620308076219,0.221672220480934,0.24672413288565,
0.272050621046898,0.282513655340624,0.286631737980665,0.311197491830502,
0.335883934863211,0.360158613898702,0.3703249274938,0.375577975829039,0.399326629202051,
0.41760862372711,0.423111147116857,0.427811294064984,0.450556480771396,
0.471648028167486,0.47402260125479),.UNSPECIFIED.);
#2101=B_SPLINE_CURVE_WITH_KNOTS('',3,(#206929,#206930,#206931,#206932,#206933,
#206934,#206935,#206936,#206937,#206938,#206939,#206940,#206941,#206942,
#206943,#206944,#206945,#206946,#206947,#206948,#206949,#206950,#206951,
#206952,#206953,#206954,#206955,#206956,#206957,#206958,#206959,#206960,
#206961,#206962,#206963,#206964,#206965,#206966,#206967,#206968,#206969,
#206970,#206971,#206972,#206973,#206974,#206975,#206976,#206977,#206978,
#206979,#206980,#206981,#206982,#206983,#206984,#206985,#206986,#206987,
#206988,#206989,#206990,#206991,#206992,#206993,#206994,#206995,#206996,
#206997,#206998,#206999,#207000,#207001,#207002,#207003,#207004,#207005,
#207006,#207007,#207008,#207009,#207010,#207011,#207012,#207013,#207014,
#207015,#207016),.UNSPECIFIED.,.F.,.F.,(4,3,3,3,3,3,3,3,3,3,3,3,3,3,3,3,
3,3,3,3,3,3,3,3,3,3,3,3,3,4),(0.,0.0223800600970233,0.045557183874987,0.0675550913477831,
0.0773343026846742,0.0821513307715598,0.086588933128813,0.110761903794659,
0.134934874460505,0.159278641767771,0.165672902158484,0.170323218744956,
0.173916080012127,0.198993337115258,0.224022472738042,0.24852272682622,
0.25855463659488,0.264135020001501,0.288903366541005,0.314991206662608,
0.341079046784212,0.351267085078404,0.355315309150301,0.381664710560744,
0.403487574104964,0.411770819428486,0.416463283580499,0.443066538814214,
0.469275862304419,0.472065635637224),.UNSPECIFIED.);
#2102=B_SPLINE_CURVE_WITH_KNOTS('',3,(#207017,#207018,#207019,#207020,#207021,
#207022,#207023,#207024,#207025,#207026,#207027,#207028,#207029,#207030,
#207031,#207032,#207033,#207034,#207035,#207036,#207037,#207038,#207039,
#207040,#207041,#207042,#207043,#207044,#207045,#207046,#207047,#207048,
#207049,#207050,#207051,#207052,#207053,#207054,#207055,#207056,#207057,
#207058,#207059,#207060,#207061,#207062,#207063,#207064,#207065,#207066,
#207067,#207068,#207069,#207070,#207071,#207072,#207073,#207074,#207075,
#207076,#207077,#207078,#207079,#207080,#207081,#207082,#207083,#207084,
#207085,#207086,#207087,#207088,#207089,#207090,#207091,#207092,#207093,
#207094,#207095,#207096,#207097,#207098,#207099,#207100,#207101),
 .UNSPECIFIED.,.F.,.F.,(4,3,3,3,3,3,3,3,3,3,3,3,3,3,3,3,3,3,3,3,3,3,3,3,
3,3,3,3,4),(0.,0.0260517912929934,0.0527225478485455,0.0776790939050551,
0.0889728021702812,0.0959464342551659,0.100845925350706,0.126855201462976,
0.152534125917849,0.176212517636641,0.192547949849574,0.196620307478408,
0.221672220182029,0.24672413288565,0.272050620811562,0.282513655553444,
0.286631738154676,0.311154771782915,0.335765993229603,0.360166884129707,
0.370324929459797,0.375577976970675,0.399326632351765,0.417608624369275,
0.423111148621278,0.427811298126592,0.450556488913046,0.471648028167475,
0.474022601254778),.UNSPECIFIED.);
#2103=B_SPLINE_CURVE_WITH_KNOTS('',3,(#207318,#207319,#207320,#207321,#207322,
#207323,#207324,#207325,#207326,#207327,#207328,#207329,#207330,#207331,
#207332,#207333,#207334,#207335,#207336,#207337,#207338,#207339,#207340,
#207341,#207342,#207343,#207344,#207345,#207346,#207347,#207348,#207349,
#207350,#207351,#207352,#207353,#207354,#207355,#207356,#207357,#207358,
#207359,#207360,#207361,#207362,#207363,#207364,#207365,#207366,#207367,
#207368,#207369,#207370,#207371,#207372,#207373,#207374,#207375,#207376,
#207377,#207378,#207379,#207380,#207381,#207382,#207383,#207384,#207385,
#207386,#207387,#207388,#207389,#207390,#207391,#207392,#207393,#207394,
#207395,#207396,#207397,#207398,#207399,#207400,#207401,#207402,#207403,
#207404,#207405,#207406,#207407,#207408,#207409,#207410,#207411,#207412,
#207413,#207414,#207415,#207416,#207417,#207418,#207419,#207420),
 .UNSPECIFIED.,.F.,.F.,(4,3,3,3,3,3,3,3,3,3,3,3,3,3,3,3,3,3,3,3,3,3,3,3,
3,3,3,3,3,3,3,3,3,3,4),(-0.950777871811442,-0.906336425390168,-0.861875033114161,
-0.842434685731619,-0.832698894406312,-0.823679279165542,-0.779911530164976,
-0.736812975118332,-0.713111655774817,-0.707528734983928,-0.706840830508988,
-0.663970529007278,-0.62096019743997,-0.578452544080758,-0.53653757030824,
-0.528618153061017,-0.5197784899906,-0.479103795974014,-0.472085166836762,
-0.430141730544578,-0.388512020610736,-0.35295009564229,-0.345831806228506,
-0.34009678874744,-0.299353453374947,-0.258818746671375,-0.246812444972861,
-0.206136253916913,-0.172639040264036,-0.165053203014642,-0.125295016427036,
-0.0858747403733512,-0.046745972523297,-0.0311581910594031,0.),
 .UNSPECIFIED.);
#2104=B_SPLINE_CURVE_WITH_KNOTS('',3,(#207421,#207422,#207423,#207424,#207425,
#207426,#207427,#207428,#207429,#207430,#207431,#207432,#207433,#207434,
#207435,#207436,#207437,#207438,#207439,#207440,#207441,#207442,#207443,
#207444,#207445,#207446,#207447,#207448,#207449,#207450,#207451,#207452,
#207453,#207454,#207455,#207456,#207457,#207458,#207459,#207460,#207461,
#207462,#207463,#207464,#207465,#207466,#207467,#207468,#207469,#207470,
#207471,#207472,#207473,#207474,#207475,#207476,#207477,#207478,#207479,
#207480,#207481,#207482,#207483,#207484,#207485,#207486,#207487,#207488,
#207489,#207490,#207491,#207492,#207493,#207494,#207495,#207496,#207497,
#207498,#207499,#207500,#207501,#207502,#207503,#207504,#207505,#207506,
#207507,#207508,#207509,#207510,#207511,#207512,#207513,#207514,#207515,
#207516,#207517,#207518,#207519,#207520,#207521,#207522,#207523),
 .UNSPECIFIED.,.F.,.F.,(4,3,3,3,3,3,3,3,3,3,3,3,3,3,3,3,3,3,3,3,3,3,3,3,
3,3,3,3,3,3,3,3,3,3,4),(0.,0.0392937243200445,0.078648792419632,0.118430422481667,
0.157174897280178,0.16530965460934,0.172511921016207,0.214141585432509,
0.254364238175765,0.295024495344819,0.335842707328534,0.340554091141284,
0.347540360366197,0.389002662438937,0.430931272514703,0.437981494075935,
0.479749916301002,0.518812960683757,0.524399035743027,0.530138494511844,
0.57262664708442,0.615529815026447,0.658476413952203,0.671400602336179,
0.691337520740504,0.703515645442784,0.711692863532045,0.721145455934051,
0.764504689623414,0.808363873685668,0.829117588621419,0.836453781446258,
0.880985314545998,0.913941349417081,0.950775682567348),.UNSPECIFIED.);
#2105=B_SPLINE_CURVE_WITH_KNOTS('',3,(#207740,#207741,#207742,#207743,#207744,
#207745,#207746,#207747,#207748,#207749,#207750,#207751,#207752,#207753,
#207754,#207755,#207756,#207757,#207758,#207759,#207760,#207761,#207762,
#207763,#207764,#207765,#207766,#207767,#207768,#207769,#207770,#207771,
#207772,#207773,#207774,#207775,#207776,#207777,#207778,#207779,#207780,
#207781,#207782,#207783,#207784,#207785,#207786,#207787,#207788,#207789,
#207790,#207791,#207792,#207793,#207794,#207795,#207796,#207797,#207798,
#207799,#207800,#207801,#207802,#207803,#207804,#207805,#207806,#207807,
#207808,#207809,#207810,#207811,#207812,#207813,#207814,#207815,#207816,
#207817,#207818,#207819,#207820,#207821,#207822,#207823,#207824,#207825,
#207826,#207827,#207828,#207829,#207830,#207831,#207832,#207833,#207834,
#207835,#207836,#207837,#207838,#207839),.UNSPECIFIED.,.F.,.F.,(4,3,3,3,
3,3,3,3,3,3,3,3,3,3,3,3,3,3,3,3,3,3,3,3,3,3,3,3,3,3,3,3,3,4),(-0.954382097139067,
-0.915540356901139,-0.875987953878927,-0.858553371309591,-0.851652578164575,
-0.844316096216611,-0.803953485084637,-0.771951682750547,-0.755904221756574,
-0.746876223962411,-0.741004834362442,-0.7398567607626,-0.698120295630557,
-0.657232380143924,-0.615071640189176,-0.572910900234428,-0.567449445615807,
-0.525372539405531,-0.515246554457167,-0.473498151147513,-0.430271385468235,
-0.387044619788958,-0.380028835408339,-0.337077765616228,-0.293664876806399,
-0.280914982302858,-0.237661647632792,-0.200416680658377,-0.194604991995093,
-0.1507164440315,-0.10637737364008,-0.0619596473409019,-0.0369876293288037,
-2.19658856801564E-6),.UNSPECIFIED.);
#2106=B_SPLINE_CURVE_WITH_KNOTS('',3,(#207840,#207841,#207842,#207843,#207844,
#207845,#207846,#207847,#207848,#207849,#207850,#207851,#207852,#207853,
#207854,#207855,#207856,#207857,#207858,#207859,#207860,#207861,#207862,
#207863,#207864,#207865,#207866,#207867,#207868,#207869,#207870,#207871,
#207872,#207873,#207874,#207875,#207876,#207877,#207878,#207879,#207880,
#207881,#207882,#207883,#207884,#207885,#207886,#207887,#207888,#207889,
#207890,#207891,#207892,#207893,#207894,#207895,#207896,#207897,#207898,
#207899,#207900,#207901,#207902,#207903,#207904,#207905,#207906,#207907,
#207908,#207909,#207910,#207911,#207912,#207913,#207914,#207915,#207916,
#207917,#207918,#207919,#207920,#207921,#207922,#207923,#207924,#207925,
#207926,#207927,#207928,#207929,#207930,#207931,#207932,#207933,#207934,
#207935,#207936,#207937,#207938,#207939,#207940,#207941,#207942),
 .UNSPECIFIED.,.F.,.F.,(4,3,3,3,3,3,3,3,3,3,3,3,3,3,3,3,3,3,3,3,3,3,3,3,
3,3,3,3,3,3,3,3,3,3,4),(3.92004242434274E-15,0.0440097382289323,0.0884882554286592,
0.132783546573759,0.176334546416905,0.187993870420512,0.19423572748739,
0.19979115047153,0.245254179237364,0.288657155098451,0.331818541228064,
0.369239411527086,0.3808541168619,0.388821225436964,0.431108255685854,0.473065176320765,
0.481013297040258,0.52321857616724,0.558979311157592,0.56811322256641,0.573516263988367,
0.614763363362682,0.655642090775697,0.696286761208482,0.70713567464641,
0.734136415169824,0.744264975553648,0.750002339682418,0.790439331413119,
0.830523899192685,0.849662847172381,0.855799185905343,0.895145184350553,
0.923141598833727,0.954382097139069),.UNSPECIFIED.);
#2107=B_SPLINE_CURVE_WITH_KNOTS('',3,(#208159,#208160,#208161,#208162,#208163,
#208164,#208165,#208166,#208167,#208168,#208169,#208170,#208171,#208172,
#208173,#208174,#208175,#208176,#208177,#208178,#208179,#208180,#208181,
#208182,#208183,#208184,#208185,#208186,#208187,#208188,#208189,#208190,
#208191,#208192,#208193,#208194,#208195,#208196,#208197,#208198,#208199,
#208200,#208201,#208202,#208203,#208204,#208205,#208206,#208207,#208208,
#208209,#208210,#208211,#208212,#208213,#208214,#208215,#208216,#208217,
#208218,#208219,#208220,#208221,#208222,#208223,#208224,#208225,#208226,
#208227,#208228,#208229,#208230,#208231,#208232,#208233,#208234,#208235,
#208236,#208237,#208238,#208239,#208240,#208241,#208242,#208243,#208244,
#208245,#208246,#208247,#208248,#208249,#208250,#208251,#208252,#208253,
#208254,#208255,#208256,#208257,#208258,#208259,#208260,#208261,#208262,
#208263,#208264),.UNSPECIFIED.,.F.,.F.,(4,3,3,3,3,3,3,3,3,3,3,3,3,3,3,3,
3,3,3,3,3,3,3,3,3,3,3,3,3,3,3,3,3,3,3,4),(-0.950777871811489,-0.90633643654385,
-0.861875036957276,-0.842434689817133,-0.831093639563838,-0.825301574638444,
-0.781525133147754,-0.738411526679356,-0.713111654821142,-0.707528734408151,
-0.70684083050903,-0.664137304886556,-0.621129293398492,-0.578512193972095,
-0.5364863625863,-0.527113744824773,-0.519453631915209,-0.479103798452372,
-0.472085166836776,-0.430141731436706,-0.38851202234129,-0.352950096664573,
-0.345831809185344,-0.340096789032849,-0.299287338987686,-0.258818748565295,
-0.246812444972867,-0.206034245191185,-0.184174738424713,-0.172639040068934,
-0.164351647577379,-0.124589561132121,-0.0849805995846697,-0.0460567214433639,
-0.0311581910594067,0.),.UNSPECIFIED.);
#2108=B_SPLINE_CURVE_WITH_KNOTS('',3,(#208265,#208266,#208267,#208268,#208269,
#208270,#208271,#208272,#208273,#208274,#208275,#208276,#208277,#208278,
#208279,#208280,#208281,#208282,#208283,#208284,#208285,#208286,#208287,
#208288,#208289,#208290,#208291,#208292,#208293,#208294,#208295,#208296,
#208297,#208298,#208299,#208300,#208301,#208302,#208303,#208304,#208305,
#208306,#208307,#208308,#208309,#208310,#208311,#208312,#208313,#208314,
#208315,#208316,#208317,#208318,#208319,#208320,#208321,#208322,#208323,
#208324,#208325,#208326,#208327,#208328,#208329,#208330,#208331,#208332,
#208333,#208334,#208335,#208336,#208337,#208338,#208339,#208340,#208341,
#208342,#208343,#208344,#208345,#208346,#208347,#208348,#208349,#208350,
#208351,#208352,#208353,#208354,#208355,#208356,#208357,#208358,#208359,
#208360,#208361,#208362,#208363,#208364,#208365,#208366,#208367),
 .UNSPECIFIED.,.F.,.F.,(4,3,3,3,3,3,3,3,3,3,3,3,3,3,3,3,3,3,3,3,3,3,3,3,
3,3,3,3,3,3,3,3,3,3,4),(2.82530270380345E-15,0.0383561142044138,0.0777322538410477,
0.117448352720408,0.157136327541592,0.16530959676955,0.172511917896846,
0.214141585432506,0.254319391003502,0.295111323821341,0.330724243378432,
0.341693770779204,0.348846513511567,0.39059233282008,0.430931232999916,
0.437981494075929,0.479749911159561,0.518812944385605,0.524709771531363,
0.530138484534004,0.572570423222229,0.615574325975759,0.658476390767529,
0.671400602336174,0.701718195721287,0.711077059751642,0.717874112270349,
0.761139330498572,0.804963166413058,0.816774798744654,0.829117599322156,
0.836453798394249,0.880985331409096,0.913941349417075,0.950775682377203),
 .UNSPECIFIED.);
#2109=B_SPLINE_CURVE_WITH_KNOTS('',3,(#208584,#208585,#208586,#208587,#208588,
#208589,#208590,#208591,#208592,#208593,#208594,#208595,#208596,#208597,
#208598,#208599,#208600,#208601,#208602,#208603,#208604,#208605,#208606,
#208607,#208608,#208609,#208610,#208611,#208612,#208613,#208614,#208615,
#208616,#208617,#208618,#208619,#208620,#208621,#208622,#208623,#208624,
#208625,#208626,#208627,#208628,#208629,#208630,#208631,#208632,#208633,
#208634,#208635,#208636,#208637,#208638,#208639,#208640,#208641,#208642,
#208643,#208644,#208645,#208646,#208647,#208648,#208649,#208650,#208651,
#208652,#208653,#208654,#208655,#208656,#208657,#208658,#208659,#208660,
#208661,#208662,#208663,#208664,#208665,#208666,#208667,#208668,#208669,
#208670,#208671,#208672,#208673,#208674,#208675,#208676,#208677,#208678,
#208679,#208680,#208681,#208682,#208683,#208684,#208685,#208686,#208687,
#208688,#208689),.UNSPECIFIED.,.F.,.F.,(4,3,3,3,3,3,3,3,3,3,3,3,3,3,3,3,
3,3,3,3,3,3,3,3,3,3,3,3,3,3,3,3,3,3,3,4),(-0.954382097139027,-0.915540393312965,
-0.875988011049171,-0.858553452015747,-0.851651720979109,-0.84431594622701,
-0.803953347308934,-0.771951616163724,-0.755904188463154,-0.746876173424658,
-0.741004793318458,-0.739856760762583,-0.698120275698938,-0.657232336987918,
-0.615071578747959,-0.572910820508001,-0.567449396059044,-0.525372472030206,
-0.515246554457162,-0.473526932909523,-0.431236741001746,-0.393744912161324,
-0.387044679913831,-0.381221890286597,-0.338027165363515,-0.294874550582207,
-0.28091498230286,-0.237709647788549,-0.212648675820495,-0.200416680015836,
-0.194604990965853,-0.150716441724806,-0.106377371171992,-0.0619596447480801,
-0.0369876293288071,-2.1968306284113E-6),.UNSPECIFIED.);
#2110=B_SPLINE_CURVE_WITH_KNOTS('',3,(#208690,#208691,#208692,#208693,#208694,
#208695,#208696,#208697,#208698,#208699,#208700,#208701,#208702,#208703,
#208704,#208705,#208706,#208707,#208708,#208709,#208710,#208711,#208712,
#208713,#208714,#208715,#208716,#208717,#208718,#208719,#208720,#208721,
#208722,#208723,#208724,#208725,#208726,#208727,#208728,#208729,#208730,
#208731,#208732,#208733,#208734,#208735,#208736,#208737,#208738,#208739,
#208740,#208741,#208742,#208743,#208744,#208745,#208746,#208747,#208748,
#208749,#208750,#208751,#208752,#208753,#208754,#208755,#208756,#208757,
#208758,#208759,#208760,#208761,#208762,#208763,#208764,#208765,#208766,
#208767,#208768,#208769,#208770,#208771,#208772,#208773,#208774,#208775,
#208776,#208777,#208778,#208779,#208780,#208781,#208782,#208783,#208784,
#208785,#208786,#208787,#208788,#208789,#208790,#208791,#208792,#208793,
#208794,#208795),.UNSPECIFIED.,.F.,.F.,(4,3,3,3,3,3,3,3,3,3,3,3,3,3,3,3,
3,3,3,3,3,3,3,3,3,3,3,3,3,3,3,3,3,3,3,4),(0.,0.0440097102619271,0.0884882277684458,
0.132783533024059,0.176334557243343,0.187993903233133,0.194235848510683,
0.199791297605252,0.245254179237363,0.288657161367001,0.331818543103485,
0.369239414789171,0.380854128970053,0.388821223648941,0.431034523258865,
0.473065169701532,0.481013297040253,0.523218575748239,0.558979309133477,
0.568113222474232,0.57351626392526,0.614765000689446,0.655861440299277,
0.696286756072865,0.707135674646407,0.734136415169823,0.74426497460981,
0.752455611749943,0.792892563063861,0.833036427815749,0.838982768060298,
0.849662831772539,0.855799161052988,0.89514516223825,0.923141598833728,
0.954382097139071),.UNSPECIFIED.);
#2111=B_SPLINE_CURVE_WITH_KNOTS('',3,(#209508,#209509,#209510,#209511,#209512,
#209513,#209514,#209515,#209516,#209517,#209518,#209519,#209520,#209521,
#209522,#209523,#209524,#209525,#209526,#209527,#209528,#209529,#209530,
#209531,#209532,#209533,#209534,#209535,#209536,#209537,#209538,#209539,
#209540,#209541,#209542,#209543,#209544,#209545,#209546,#209547,#209548,
#209549,#209550,#209551,#209552,#209553,#209554,#209555,#209556,#209557,
#209558,#209559,#209560,#209561,#209562,#209563,#209564,#209565,#209566,
#209567,#209568,#209569,#209570,#209571,#209572,#209573,#209574,#209575,
#209576,#209577,#209578,#209579,#209580,#209581,#209582,#209583,#209584,
#209585,#209586,#209587,#209588,#209589,#209590,#209591,#209592,#209593,
#209594,#209595),.UNSPECIFIED.,.F.,.F.,(4,3,3,3,3,3,3,3,3,3,3,3,3,3,3,3,
3,3,3,3,3,3,3,3,3,3,3,3,3,4),(0.,0.0223800415826111,0.0455571510723243,
0.0675550609170155,0.0773342741558292,0.0821512675008773,0.0865889126878389,
0.11057788386222,0.135008172941507,0.157206745152612,0.16567286565653,0.170323051943897,
0.173915800266865,0.198993060769186,0.224022472738035,0.248477223249604,
0.258554635986008,0.264135020444879,0.28890337893006,0.314991216050641,
0.341079053171223,0.351267091230857,0.355315312478378,0.381664715071331,
0.403487578818942,0.410694480570935,0.416463278950785,0.443066534470941,
0.469275862304353,0.472065636725432),.UNSPECIFIED.);
#2112=B_SPLINE_CURVE_WITH_KNOTS('',3,(#210308,#210309,#210310,#210311,#210312,
#210313,#210314,#210315,#210316,#210317,#210318,#210319,#210320,#210321,
#210322,#210323,#210324,#210325,#210326,#210327,#210328,#210329,#210330,
#210331,#210332,#210333,#210334,#210335,#210336,#210337,#210338,#210339,
#210340,#210341,#210342,#210343,#210344,#210345,#210346,#210347,#210348,
#210349,#210350,#210351,#210352,#210353,#210354,#210355,#210356,#210357,
#210358,#210359,#210360,#210361,#210362,#210363,#210364,#210365,#210366,
#210367,#210368,#210369,#210370,#210371,#210372,#210373,#210374,#210375,
#210376,#210377,#210378,#210379,#210380,#210381,#210382,#210383,#210384,
#210385,#210386,#210387,#210388,#210389,#210390,#210391,#210392,#210393,
#210394,#210395,#210396,#210397,#210398),.UNSPECIFIED.,.F.,.F.,(4,3,3,3,
3,3,3,3,3,3,3,3,3,3,3,3,3,3,3,3,3,3,3,3,3,3,3,3,3,3,4),(7.90123170449159E-15,
0.0260517808136012,0.0527225352991877,0.0776790852361114,0.0889727992741923,
0.0959464344241781,0.100845925040092,0.126855201361835,0.152534129667343,
0.17621251994363,0.186122361828502,0.19254794682658,0.196620306433238,0.221672219659448,
0.246724132885659,0.272058447969215,0.280886246322291,0.285802388610614,
0.299566540114185,0.311229550951507,0.33591592242145,0.360190200940758,
0.370324932919906,0.375577978970566,0.399326637919175,0.417608625494232,
0.423111151172439,0.427811304835429,0.450556502779002,0.471648028167516,
0.474022601254811),.UNSPECIFIED.);
#2113=B_SPLINE_CURVE_WITH_KNOTS('',3,(#211111,#211112,#211113,#211114,#211115,
#211116,#211117,#211118,#211119,#211120,#211121,#211122,#211123,#211124,
#211125,#211126,#211127,#211128,#211129,#211130,#211131,#211132,#211133,
#211134,#211135,#211136,#211137,#211138,#211139,#211140,#211141,#211142,
#211143,#211144,#211145,#211146,#211147,#211148,#211149,#211150,#211151,
#211152,#211153,#211154,#211155,#211156,#211157,#211158,#211159,#211160,
#211161,#211162,#211163,#211164,#211165,#211166,#211167,#211168,#211169,
#211170,#211171,#211172,#211173,#211174,#211175,#211176,#211177,#211178,
#211179,#211180,#211181,#211182,#211183,#211184,#211185,#211186,#211187,
#211188,#211189,#211190,#211191,#211192,#211193,#211194,#211195,#211196,
#211197,#211198),.UNSPECIFIED.,.F.,.F.,(4,3,3,3,3,3,3,3,3,3,3,3,3,3,3,3,
3,3,3,3,3,3,3,3,3,3,3,3,3,4),(0.,0.022380064656475,0.0455571919885892,0.0675550989125488,
0.077334309776642,0.0821513465008637,0.0865889382889745,0.110577925353253,
0.135008216273016,0.157206781258753,0.165672911295151,0.170323260534971,
0.173916149941423,0.198993406189961,0.22402247273804,0.248477212094458,
0.258554636746328,0.26413501995488,0.288903363466092,0.314991204360096,
0.341079045254099,0.351267083567837,0.355315308310309,0.381664709440852,
0.403487572943969,0.410694455370546,0.416463284762423,0.443066539898884,
0.469275862304369,0.472065635365967),.UNSPECIFIED.);
#2114=B_SPLINE_CURVE_WITH_KNOTS('',3,(#211911,#211912,#211913,#211914,#211915,
#211916,#211917,#211918,#211919,#211920,#211921,#211922,#211923,#211924,
#211925,#211926,#211927,#211928,#211929,#211930,#211931,#211932,#211933,
#211934,#211935,#211936,#211937,#211938,#211939,#211940,#211941,#211942,
#211943,#211944,#211945,#211946,#211947,#211948,#211949,#211950,#211951,
#211952,#211953,#211954,#211955,#211956,#211957,#211958,#211959,#211960,
#211961,#211962,#211963,#211964,#211965,#211966,#211967,#211968,#211969,
#211970,#211971,#211972,#211973,#211974,#211975,#211976,#211977,#211978,
#211979,#211980,#211981,#211982,#211983,#211984,#211985,#211986,#211987,
#211988,#211989,#211990,#211991,#211992,#211993,#211994,#211995,#211996,
#211997,#211998),.UNSPECIFIED.,.F.,.F.,(4,3,3,3,3,3,3,3,3,3,3,3,3,3,3,3,
3,3,3,3,3,3,3,3,3,3,3,3,3,4),(0.,0.026051775604345,0.0527225290853877,0.0776790809548157,
0.0889727978441528,0.0959464345074647,0.10084592486155,0.126855201263961,
0.152534131465872,0.176212521061365,0.186122361876941,0.192547945329784,
0.196620305916515,0.221672219401092,0.246724132885669,0.27206158277579,
0.282513656118586,0.286631738568381,0.311197492372781,0.335883935062334,
0.360158620947264,0.370324934628168,0.375577979963716,0.399595492014671,
0.417608626052888,0.423111152459427,0.427811308268704,0.45055650974011,
0.471648028167537,0.474022601254832),.UNSPECIFIED.);
#2115=B_SPLINE_CURVE_WITH_KNOTS('',3,(#212711,#212712,#212713,#212714,#212715,
#212716,#212717,#212718,#212719,#212720,#212721,#212722,#212723,#212724,
#212725,#212726,#212727,#212728,#212729,#212730,#212731,#212732,#212733,
#212734,#212735,#212736,#212737,#212738,#212739,#212740,#212741,#212742,
#212743,#212744,#212745,#212746,#212747,#212748,#212749,#212750,#212751,
#212752,#212753,#212754,#212755,#212756,#212757,#212758,#212759,#212760,
#212761,#212762,#212763,#212764,#212765,#212766,#212767,#212768,#212769,
#212770,#212771,#212772,#212773,#212774,#212775,#212776,#212777,#212778,
#212779,#212780,#212781,#212782,#212783,#212784,#212785,#212786,#212787,
#212788,#212789,#212790,#212791,#212792,#212793,#212794,#212795,#212796,
#212797,#212798),.UNSPECIFIED.,.F.,.F.,(4,3,3,3,3,3,3,3,3,3,3,3,3,3,3,3,
3,3,3,3,3,3,3,3,3,3,3,3,3,4),(0.,0.0223800651370331,0.0455571928568673,
0.0675550997304994,0.0773343105434705,0.0833848318194916,0.0865889388358174,
0.110577926266239,0.135008217226555,0.157206782032257,0.165672912272975,
0.170323265017005,0.173916157466764,0.198993413622444,0.224022472738036,
0.248477211854248,0.258554636762497,0.264135019948427,0.28898134258909,
0.314338830544068,0.340111642432823,0.351267083403808,0.355315308234309,
0.381664709331105,0.403487572828058,0.410694454865743,0.416463284884501,
0.443066539997533,0.469275862304369,0.472065635336616),.UNSPECIFIED.);
#2116=B_SPLINE_CURVE_WITH_KNOTS('',3,(#213511,#213512,#213513,#213514,#213515,
#213516,#213517,#213518,#213519,#213520,#213521,#213522,#213523,#213524,
#213525,#213526,#213527,#213528,#213529,#213530,#213531,#213532,#213533,
#213534,#213535,#213536,#213537,#213538,#213539,#213540,#213541,#213542,
#213543,#213544,#213545,#213546,#213547,#213548,#213549,#213550,#213551,
#213552,#213553,#213554,#213555,#213556,#213557,#213558,#213559,#213560,
#213561,#213562,#213563,#213564,#213565,#213566,#213567,#213568,#213569,
#213570,#213571,#213572,#213573,#213574,#213575,#213576,#213577,#213578,
#213579,#213580,#213581,#213582,#213583,#213584,#213585,#213586,#213587,
#213588,#213589,#213590,#213591,#213592,#213593,#213594,#213595,#213596,
#213597,#213598),.UNSPECIFIED.,.F.,.F.,(4,3,3,3,3,3,3,3,3,3,3,3,3,3,3,3,
3,3,3,3,3,3,3,3,3,3,3,3,3,4),(0.,0.0261324658014236,0.0526962913261088,
0.0793415357281651,0.0889727984346616,0.095835043250178,0.10084592493607,
0.126856858695135,0.152713978120786,0.17794985603476,0.186122361857045,
0.192547945950156,0.196620306130287,0.221672219507975,0.246724132885664,
0.272050620322494,0.282513656041832,0.286631738502527,0.311258832154326,
0.335885925806125,0.360166888882926,0.37032493392055,0.375577979558784,
0.399326639542124,0.417608625825101,0.423111151926387,0.42781130682219,
0.45055650683662,0.47164802816751,0.474022601254803),.UNSPECIFIED.);
#2117=B_SPLINE_CURVE_WITH_KNOTS('',3,(#214311,#214312,#214313,#214314,#214315,
#214316,#214317,#214318,#214319,#214320,#214321,#214322,#214323,#214324,
#214325,#214326,#214327,#214328,#214329,#214330,#214331,#214332,#214333,
#214334,#214335,#214336,#214337,#214338,#214339,#214340,#214341,#214342,
#214343,#214344,#214345,#214346,#214347,#214348,#214349,#214350,#214351,
#214352,#214353,#214354,#214355,#214356,#214357,#214358,#214359,#214360,
#214361,#214362,#214363,#214364,#214365,#214366,#214367,#214368,#214369,
#214370,#214371,#214372,#214373,#214374,#214375,#214376,#214377,#214378,
#214379,#214380,#214381,#214382,#214383,#214384,#214385,#214386,#214387,
#214388,#214389,#214390,#214391,#214392,#214393,#214394,#214395),
 .UNSPECIFIED.,.F.,.F.,(4,3,3,3,3,3,3,3,3,3,3,3,3,3,3,3,3,3,3,3,3,3,3,3,
3,3,3,3,4),(0.,0.0222914007901619,0.0454674359825707,0.0675550870544155,
0.0821513218453204,0.0865889302954898,0.110629677084235,0.134994651844209,
0.159338030720047,0.165672897048461,0.170323195429502,0.173916040779313,
0.19899329834446,0.224022472738044,0.248477215576034,0.258554636508914,
0.264135020109551,0.288903368301885,0.314991208014035,0.341079047726185,
0.351267085960766,0.355315309607254,0.381664711215564,0.4034875747766,0.410694463232085,
0.416463282945419,0.443066538202943,0.469275862304378,0.472065635791059),
 .UNSPECIFIED.);
#2118=B_SPLINE_CURVE_WITH_KNOTS('',3,(#215108,#215109,#215110,#215111,#215112,
#215113,#215114,#215115,#215116,#215117,#215118,#215119,#215120,#215121,
#215122,#215123,#215124,#215125,#215126,#215127,#215128,#215129,#215130,
#215131,#215132,#215133,#215134,#215135,#215136,#215137,#215138,#215139,
#215140,#215141,#215142,#215143,#215144,#215145,#215146,#215147,#215148,
#215149,#215150,#215151,#215152,#215153,#215154,#215155,#215156,#215157,
#215158,#215159,#215160,#215161,#215162,#215163,#215164,#215165,#215166,
#215167,#215168,#215169,#215170,#215171,#215172,#215173,#215174,#215175,
#215176,#215177,#215178,#215179,#215180,#215181,#215182,#215183,#215184,
#215185,#215186,#215187,#215188,#215189,#215190,#215191,#215192,#215193,
#215194,#215195),.UNSPECIFIED.,.F.,.F.,(4,3,3,3,3,3,3,3,3,3,3,3,3,3,3,3,
3,3,3,3,3,3,3,3,3,3,3,3,3,4),(7.97682625883415E-15,0.0260517932991795,0.0527225502147213,
0.077679095575174,0.0889728027275484,0.0959464342222353,0.10084592545247,
0.126855201609306,0.152534125302762,0.176212517229938,0.186122361708183,
0.19254795046146,0.196620307684512,0.221672220285089,0.246724132885667,
0.272050620894862,0.282513655479386,0.286631738114849,0.31115477174714,
0.335765993047061,0.360166883426141,0.370324928797177,0.375577976589965,
0.399326631291424,0.417608624155145,0.423111148097321,0.427811296634432,
0.450556486039326,0.47164802816752,0.474022601254815),.UNSPECIFIED.);
#2127=SHAPE_REPRESENTATION_RELATIONSHIP('SRR','None',#215652,#2136);
#2136=ADVANCED_BREP_SHAPE_REPRESENTATION('',(#2154),#215608);
#2145=STYLED_ITEM('',(#215698),#2154);
#2154=MANIFOLD_SOLID_BREP('Body1',#28088);
#2689=CYLINDRICAL_SURFACE('',#29721,5.099);
#2690=CYLINDRICAL_SURFACE('',#29723,5.099);
#2691=CYLINDRICAL_SURFACE('',#29724,5.099);
#2692=CYLINDRICAL_SURFACE('',#29725,5.099);
#2693=CYLINDRICAL_SURFACE('',#29726,5.099);
#2694=CYLINDRICAL_SURFACE('',#29728,5.099);
#2695=CYLINDRICAL_SURFACE('',#29729,5.099);
#2696=CYLINDRICAL_SURFACE('',#29730,5.099);
#2697=CYLINDRICAL_SURFACE('',#29731,2.55999999999999);
#2698=CYLINDRICAL_SURFACE('',#29733,2.55999999999999);
#2699=CYLINDRICAL_SURFACE('',#29734,2.55999999999999);
#2700=CYLINDRICAL_SURFACE('',#29735,2.55999999999999);
#2701=CYLINDRICAL_SURFACE('',#29736,2.55999999999999);
#2702=CYLINDRICAL_SURFACE('',#29737,2.55999999999999);
#2703=CYLINDRICAL_SURFACE('',#29738,2.55999999999999);
#2704=CYLINDRICAL_SURFACE('',#29739,2.55999999999999);
#2705=CYLINDRICAL_SURFACE('',#29740,2.55999999999999);
#2706=CYLINDRICAL_SURFACE('',#29741,2.55999999999999);
#2707=CYLINDRICAL_SURFACE('',#29742,2.55999999999999);
#2708=CYLINDRICAL_SURFACE('',#29743,2.55999999999999);
#2709=CYLINDRICAL_SURFACE('',#29744,2.55999999999999);
#2710=CYLINDRICAL_SURFACE('',#29745,2.55999999999999);
#2711=CYLINDRICAL_SURFACE('',#29746,2.55999999999999);
#2712=CYLINDRICAL_SURFACE('',#29747,2.55999999999999);
#2713=CYLINDRICAL_SURFACE('',#29748,2.55999999999999);
#2714=CYLINDRICAL_SURFACE('',#29749,2.55999999999999);
#2715=CYLINDRICAL_SURFACE('',#29750,2.55999999999999);
#2716=CYLINDRICAL_SURFACE('',#29751,2.55999999999999);
#2717=CYLINDRICAL_SURFACE('',#29752,2.55999999999999);
#2718=CYLINDRICAL_SURFACE('',#29753,2.55999999999999);
#2719=CYLINDRICAL_SURFACE('',#29754,2.55999999999999);
#2720=CYLINDRICAL_SURFACE('',#29755,2.55999999999999);
#2721=CYLINDRICAL_SURFACE('',#29756,2.55999999999999);
#2722=CYLINDRICAL_SURFACE('',#29757,2.55999999999999);
#2723=CYLINDRICAL_SURFACE('',#29758,2.55999999999999);
#2724=CYLINDRICAL_SURFACE('',#29759,2.56);
#2725=CYLINDRICAL_SURFACE('',#29761,2.56);
#2726=CYLINDRICAL_SURFACE('',#29762,2.56);
#2727=CYLINDRICAL_SURFACE('',#29763,2.56);
#2728=CYLINDRICAL_SURFACE('',#29764,2.56);
#2729=CYLINDRICAL_SURFACE('',#29765,2.56);
#2730=CYLINDRICAL_SURFACE('',#29766,2.56);
#2731=CYLINDRICAL_SURFACE('',#29767,2.56);
#2732=CYLINDRICAL_SURFACE('',#29768,2.56);
#2733=CYLINDRICAL_SURFACE('',#29769,2.56);
#2734=CYLINDRICAL_SURFACE('',#29770,2.56);
#2735=CYLINDRICAL_SURFACE('',#29771,2.56);
#2736=CYLINDRICAL_SURFACE('',#29772,2.56);
#2737=CYLINDRICAL_SURFACE('',#29773,2.56);
#2738=CYLINDRICAL_SURFACE('',#29774,2.56);
#2739=CYLINDRICAL_SURFACE('',#29775,2.56);
#2740=CYLINDRICAL_SURFACE('',#29776,2.56);
#2741=CYLINDRICAL_SURFACE('',#29777,2.56);
#2742=CYLINDRICAL_SURFACE('',#29778,2.56);
#2743=CYLINDRICAL_SURFACE('',#29779,2.56);
#2744=CYLINDRICAL_SURFACE('',#29780,2.56);
#2745=CYLINDRICAL_SURFACE('',#29781,2.56);
#2746=CYLINDRICAL_SURFACE('',#29782,2.56);
#2747=CYLINDRICAL_SURFACE('',#29783,2.56);
#2748=CYLINDRICAL_SURFACE('',#29784,2.56);
#2749=CYLINDRICAL_SURFACE('',#29785,2.56);
#2750=CYLINDRICAL_SURFACE('',#29786,2.56);
#2751=CYLINDRICAL_SURFACE('',#29787,2.56);
#2752=CYLINDRICAL_SURFACE('',#29789,2.56);
#2753=CYLINDRICAL_SURFACE('',#29790,2.56);
#2754=CYLINDRICAL_SURFACE('',#29791,2.56);
#2755=CYLINDRICAL_SURFACE('',#29792,2.56);
#2756=CYLINDRICAL_SURFACE('',#29793,2.56);
#2757=CYLINDRICAL_SURFACE('',#29794,2.56);
#2758=CYLINDRICAL_SURFACE('',#29795,2.56);
#2759=CYLINDRICAL_SURFACE('',#29796,2.56);
#2760=CYLINDRICAL_SURFACE('',#29797,2.56);
#2761=CYLINDRICAL_SURFACE('',#29798,2.56);
#2762=CYLINDRICAL_SURFACE('',#29799,2.56);
#2763=CYLINDRICAL_SURFACE('',#29800,2.56);
#2764=CYLINDRICAL_SURFACE('',#29801,2.56);
#2765=CYLINDRICAL_SURFACE('',#29802,2.56);
#2766=CYLINDRICAL_SURFACE('',#29803,2.56);
#2767=CYLINDRICAL_SURFACE('',#29804,2.56);
#2768=CYLINDRICAL_SURFACE('',#29805,2.56);
#2769=CYLINDRICAL_SURFACE('',#29806,2.56);
#2770=CYLINDRICAL_SURFACE('',#29807,2.56);
#2771=CYLINDRICAL_SURFACE('',#29808,2.56);
#2772=CYLINDRICAL_SURFACE('',#29809,2.56);
#2773=CYLINDRICAL_SURFACE('',#29810,2.56);
#2774=CYLINDRICAL_SURFACE('',#29811,2.56);
#2775=CYLINDRICAL_SURFACE('',#29812,2.56);
#2776=CYLINDRICAL_SURFACE('',#29813,2.56);
#2777=CYLINDRICAL_SURFACE('',#29814,2.56);
#2778=CYLINDRICAL_SURFACE('',#29815,2.56);
#2779=CYLINDRICAL_SURFACE('',#29817,2.56);
#2780=CYLINDRICAL_SURFACE('',#29818,2.56);
#2781=CYLINDRICAL_SURFACE('',#29819,2.56);
#2782=CYLINDRICAL_SURFACE('',#29820,2.56);
#2783=CYLINDRICAL_SURFACE('',#29821,2.56);
#2784=CYLINDRICAL_SURFACE('',#29822,2.56);
#2785=CYLINDRICAL_SURFACE('',#29823,2.56);
#2786=CYLINDRICAL_SURFACE('',#29824,2.56);
#2787=CYLINDRICAL_SURFACE('',#29825,2.56);
#2788=CYLINDRICAL_SURFACE('',#29826,2.56);
#2789=CYLINDRICAL_SURFACE('',#29827,2.56);
#2790=CYLINDRICAL_SURFACE('',#29828,2.56);
#2791=CYLINDRICAL_SURFACE('',#29829,2.56);
#2792=CYLINDRICAL_SURFACE('',#29830,2.56);
#2793=CYLINDRICAL_SURFACE('',#29831,2.56);
#2794=CYLINDRICAL_SURFACE('',#29832,2.56);
#2795=CYLINDRICAL_SURFACE('',#29833,2.56);
#2796=CYLINDRICAL_SURFACE('',#29834,2.56);
#2797=CYLINDRICAL_SURFACE('',#29835,2.56);
#2798=CYLINDRICAL_SURFACE('',#29836,2.56);
#2799=CYLINDRICAL_SURFACE('',#29837,2.56);
#2800=CYLINDRICAL_SURFACE('',#29838,2.56);
#2801=CYLINDRICAL_SURFACE('',#29839,2.56);
#2802=CYLINDRICAL_SURFACE('',#29840,2.56);
#2803=CYLINDRICAL_SURFACE('',#29841,2.56);
#2804=CYLINDRICAL_SURFACE('',#29842,2.56);
#2805=CYLINDRICAL_SURFACE('',#29843,4.263);
#2806=CYLINDRICAL_SURFACE('',#29845,4.263);
#2807=CYLINDRICAL_SURFACE('',#29847,4.263);
#2808=CYLINDRICAL_SURFACE('',#29848,4.263);
#2809=CYLINDRICAL_SURFACE('',#29849,4.263);
#2810=CYLINDRICAL_SURFACE('',#29851,4.263);
#2811=CYLINDRICAL_SURFACE('',#29852,4.263);
#2812=CYLINDRICAL_SURFACE('',#29853,4.263);
#2813=CYLINDRICAL_SURFACE('',#29855,2.117);
#2814=CYLINDRICAL_SURFACE('',#29857,2.117);
#2815=CYLINDRICAL_SURFACE('',#29858,2.117);
#2816=CYLINDRICAL_SURFACE('',#29859,2.117);
#2817=CYLINDRICAL_SURFACE('',#29860,2.117);
#2818=CYLINDRICAL_SURFACE('',#29861,2.117);
#2819=CYLINDRICAL_SURFACE('',#29862,2.117);
#2820=CYLINDRICAL_SURFACE('',#29863,2.117);
#2821=CYLINDRICAL_SURFACE('',#29864,2.117);
#2822=CYLINDRICAL_SURFACE('',#29865,2.117);
#2823=CYLINDRICAL_SURFACE('',#29866,2.117);
#2824=CYLINDRICAL_SURFACE('',#29867,2.117);
#2825=CYLINDRICAL_SURFACE('',#29868,2.117);
#2826=CYLINDRICAL_SURFACE('',#29869,2.117);
#2827=CYLINDRICAL_SURFACE('',#29870,2.117);
#2828=CYLINDRICAL_SURFACE('',#29871,2.117);
#2829=CYLINDRICAL_SURFACE('',#29872,2.117);
#2830=CYLINDRICAL_SURFACE('',#29873,2.117);
#2831=CYLINDRICAL_SURFACE('',#29874,2.117);
#2832=CYLINDRICAL_SURFACE('',#29875,2.117);
#2833=CYLINDRICAL_SURFACE('',#29876,2.117);
#2834=CYLINDRICAL_SURFACE('',#29877,2.117);
#2835=CYLINDRICAL_SURFACE('',#29878,2.117);
#2836=CYLINDRICAL_SURFACE('',#29879,2.117);
#2837=CYLINDRICAL_SURFACE('',#29880,2.117);
#2838=CYLINDRICAL_SURFACE('',#29881,2.117);
#2839=CYLINDRICAL_SURFACE('',#29882,2.117);
#2840=CYLINDRICAL_SURFACE('',#29883,2.117);
#2841=CYLINDRICAL_SURFACE('',#29885,2.117);
#2842=CYLINDRICAL_SURFACE('',#29886,2.117);
#2843=CYLINDRICAL_SURFACE('',#29887,2.117);
#2844=CYLINDRICAL_SURFACE('',#29888,2.117);
#2845=CYLINDRICAL_SURFACE('',#29889,2.117);
#2846=CYLINDRICAL_SURFACE('',#29890,2.117);
#2847=CYLINDRICAL_SURFACE('',#29891,2.117);
#2848=CYLINDRICAL_SURFACE('',#29892,2.117);
#2849=CYLINDRICAL_SURFACE('',#29893,2.117);
#2850=CYLINDRICAL_SURFACE('',#29894,2.117);
#2851=CYLINDRICAL_SURFACE('',#29895,2.117);
#2852=CYLINDRICAL_SURFACE('',#29896,2.117);
#2853=CYLINDRICAL_SURFACE('',#29897,2.117);
#2854=CYLINDRICAL_SURFACE('',#29898,2.117);
#2855=CYLINDRICAL_SURFACE('',#29899,2.117);
#2856=CYLINDRICAL_SURFACE('',#29900,2.117);
#2857=CYLINDRICAL_SURFACE('',#29901,2.117);
#2858=CYLINDRICAL_SURFACE('',#29902,2.117);
#2859=CYLINDRICAL_SURFACE('',#29903,2.117);
#2860=CYLINDRICAL_SURFACE('',#29904,2.117);
#2861=CYLINDRICAL_SURFACE('',#29905,2.117);
#2862=CYLINDRICAL_SURFACE('',#29906,2.117);
#2863=CYLINDRICAL_SURFACE('',#29907,2.117);
#2864=CYLINDRICAL_SURFACE('',#29908,2.117);
#2865=CYLINDRICAL_SURFACE('',#29909,2.117);
#2866=CYLINDRICAL_SURFACE('',#29910,2.117);
#2867=CYLINDRICAL_SURFACE('',#29911,2.117);
#2868=CYLINDRICAL_SURFACE('',#29913,2.117);
#2869=CYLINDRICAL_SURFACE('',#29914,2.117);
#2870=CYLINDRICAL_SURFACE('',#29915,2.117);
#2871=CYLINDRICAL_SURFACE('',#29916,2.117);
#2872=CYLINDRICAL_SURFACE('',#29917,2.117);
#2873=CYLINDRICAL_SURFACE('',#29918,2.117);
#2874=CYLINDRICAL_SURFACE('',#29919,2.117);
#2875=CYLINDRICAL_SURFACE('',#29920,2.117);
#2876=CYLINDRICAL_SURFACE('',#29921,2.117);
#2877=CYLINDRICAL_SURFACE('',#29922,2.117);
#2878=CYLINDRICAL_SURFACE('',#29923,2.117);
#2879=CYLINDRICAL_SURFACE('',#29924,2.117);
#2880=CYLINDRICAL_SURFACE('',#29925,2.117);
#2881=CYLINDRICAL_SURFACE('',#29926,2.117);
#2882=CYLINDRICAL_SURFACE('',#29927,2.117);
#2883=CYLINDRICAL_SURFACE('',#29928,2.117);
#2884=CYLINDRICAL_SURFACE('',#29929,2.117);
#2885=CYLINDRICAL_SURFACE('',#29930,2.117);
#2886=CYLINDRICAL_SURFACE('',#29931,2.117);
#2887=CYLINDRICAL_SURFACE('',#29932,2.117);
#2888=CYLINDRICAL_SURFACE('',#29933,2.117);
#2889=CYLINDRICAL_SURFACE('',#29934,2.117);
#2890=CYLINDRICAL_SURFACE('',#29935,2.117);
#2891=CYLINDRICAL_SURFACE('',#29936,2.117);
#2892=CYLINDRICAL_SURFACE('',#29937,2.117);
#2893=CYLINDRICAL_SURFACE('',#29938,2.117);
#2894=CYLINDRICAL_SURFACE('',#29939,2.117);
#2895=CYLINDRICAL_SURFACE('',#29941,2.117);
#2896=CYLINDRICAL_SURFACE('',#29942,2.117);
#2897=CYLINDRICAL_SURFACE('',#29943,2.117);
#2898=CYLINDRICAL_SURFACE('',#29944,2.117);
#2899=CYLINDRICAL_SURFACE('',#29945,2.117);
#2900=CYLINDRICAL_SURFACE('',#29946,2.117);
#2901=CYLINDRICAL_SURFACE('',#29947,2.117);
#2902=CYLINDRICAL_SURFACE('',#29948,2.117);
#2903=CYLINDRICAL_SURFACE('',#29949,2.117);
#2904=CYLINDRICAL_SURFACE('',#29950,2.117);
#2905=CYLINDRICAL_SURFACE('',#29951,2.117);
#2906=CYLINDRICAL_SURFACE('',#29952,2.117);
#2907=CYLINDRICAL_SURFACE('',#29953,2.117);
#2908=CYLINDRICAL_SURFACE('',#29954,2.117);
#2909=CYLINDRICAL_SURFACE('',#29955,2.117);
#2910=CYLINDRICAL_SURFACE('',#29956,2.117);
#2911=CYLINDRICAL_SURFACE('',#29957,2.117);
#2912=CYLINDRICAL_SURFACE('',#29958,2.117);
#2913=CYLINDRICAL_SURFACE('',#29959,2.117);
#2914=CYLINDRICAL_SURFACE('',#29960,2.117);
#2915=CYLINDRICAL_SURFACE('',#29961,2.117);
#2916=CYLINDRICAL_SURFACE('',#29962,2.117);
#2917=CYLINDRICAL_SURFACE('',#29963,2.117);
#2918=CYLINDRICAL_SURFACE('',#29964,2.117);
#2919=CYLINDRICAL_SURFACE('',#29965,2.117);
#2920=CYLINDRICAL_SURFACE('',#29966,2.117);
#2921=CYLINDRICAL_SURFACE('',#29967,2.117);
#2922=CYLINDRICAL_SURFACE('',#29969,2.117);
#2923=CYLINDRICAL_SURFACE('',#29971,2.117);
#2924=CYLINDRICAL_SURFACE('',#29973,2.117);
#2925=CYLINDRICAL_SURFACE('',#29975,4.263);
#2926=CYLINDRICAL_SURFACE('',#29977,4.263);
#2927=CYLINDRICAL_SURFACE('',#29979,2.56);
#2928=CYLINDRICAL_SURFACE('',#29981,2.56);
#2929=CYLINDRICAL_SURFACE('',#29983,2.56);
#2930=CYLINDRICAL_SURFACE('',#29985,2.55999999999999);
#2931=CYLINDRICAL_SURFACE('',#29987,5.099);
#2932=CYLINDRICAL_SURFACE('',#29989,5.099);
#2933=CYLINDRICAL_SURFACE('',#29991,4.);
#2934=CYLINDRICAL_SURFACE('',#29995,4.5);
#2935=CYLINDRICAL_SURFACE('',#30000,4.);
#2936=CYLINDRICAL_SURFACE('',#30004,4.5);
#2937=CYLINDRICAL_SURFACE('',#30009,5.);
#2938=CYLINDRICAL_SURFACE('',#30036,3.);
#2939=CYLINDRICAL_SURFACE('',#30040,6.);
#2940=CYLINDRICAL_SURFACE('',#30044,6.);
#2941=CYLINDRICAL_SURFACE('',#30059,3.);
#2942=CYLINDRICAL_SURFACE('',#30065,4.);
#2943=CYLINDRICAL_SURFACE('',#30069,5.);
#2944=CYLINDRICAL_SURFACE('',#30072,6.);
#2945=CYLINDRICAL_SURFACE('',#30076,6.);
#2946=CYLINDRICAL_SURFACE('',#30091,3.);
#2947=CYLINDRICAL_SURFACE('',#30102,3.);
#2948=CYLINDRICAL_SURFACE('',#30110,5.);
#2949=CYLINDRICAL_SURFACE('',#30113,4.);
#2950=CYLINDRICAL_SURFACE('',#30116,2.5);
#2951=CYLINDRICAL_SURFACE('',#30119,2.5);
#2952=CYLINDRICAL_SURFACE('',#30123,3.99143708455989);
#2953=CYLINDRICAL_SURFACE('',#30125,0.190999999999999);
#2954=CYLINDRICAL_SURFACE('',#30128,0.190999999999999);
#2955=CYLINDRICAL_SURFACE('',#30131,0.254);
#2956=CYLINDRICAL_SURFACE('',#30134,5.);
#2957=CYLINDRICAL_SURFACE('',#30136,5.);
#2958=CYLINDRICAL_SURFACE('',#30139,5.);
#2959=CYLINDRICAL_SURFACE('',#30142,5.);
#2960=CYLINDRICAL_SURFACE('',#30145,0.253999999999999);
#2961=CYLINDRICAL_SURFACE('',#30148,0.190999999999999);
#2962=CYLINDRICAL_SURFACE('',#30151,0.191);
#2963=CYLINDRICAL_SURFACE('',#30154,3.9914370845599);
#3917=FACE_OUTER_BOUND('',#5277,.T.);
#3918=FACE_OUTER_BOUND('',#5278,.T.);
#3919=FACE_OUTER_BOUND('',#5279,.T.);
#3920=FACE_OUTER_BOUND('',#5280,.T.);
#3921=FACE_OUTER_BOUND('',#5281,.T.);
#3922=FACE_OUTER_BOUND('',#5282,.T.);
#3923=FACE_OUTER_BOUND('',#5283,.T.);
#3924=FACE_OUTER_BOUND('',#5284,.T.);
#3925=FACE_OUTER_BOUND('',#5285,.T.);
#3926=FACE_OUTER_BOUND('',#5286,.T.);
#3927=FACE_OUTER_BOUND('',#5287,.T.);
#3928=FACE_OUTER_BOUND('',#5288,.T.);
#3929=FACE_OUTER_BOUND('',#5289,.T.);
#3930=FACE_OUTER_BOUND('',#5290,.T.);
#3931=FACE_OUTER_BOUND('',#5291,.T.);
#3932=FACE_OUTER_BOUND('',#5292,.T.);
#3933=FACE_OUTER_BOUND('',#5293,.T.);
#3934=FACE_OUTER_BOUND('',#5294,.T.);
#3935=FACE_OUTER_BOUND('',#5295,.T.);
#3936=FACE_OUTER_BOUND('',#5296,.T.);
#3937=FACE_OUTER_BOUND('',#5297,.T.);
#3938=FACE_OUTER_BOUND('',#5298,.T.);
#3939=FACE_OUTER_BOUND('',#5299,.T.);
#3940=FACE_OUTER_BOUND('',#5300,.T.);
#3941=FACE_OUTER_BOUND('',#5301,.T.);
#3942=FACE_OUTER_BOUND('',#5302,.T.);
#3943=FACE_OUTER_BOUND('',#5303,.T.);
#3944=FACE_OUTER_BOUND('',#5304,.T.);
#3945=FACE_OUTER_BOUND('',#5305,.T.);
#3946=FACE_OUTER_BOUND('',#5306,.T.);
#3947=FACE_OUTER_BOUND('',#5307,.T.);
#3948=FACE_OUTER_BOUND('',#5308,.T.);
#3949=FACE_OUTER_BOUND('',#5309,.T.);
#3950=FACE_OUTER_BOUND('',#5310,.T.);
#3951=FACE_OUTER_BOUND('',#5311,.T.);
#3952=FACE_OUTER_BOUND('',#5312,.T.);
#3953=FACE_OUTER_BOUND('',#5313,.T.);
#3954=FACE_OUTER_BOUND('',#5314,.T.);
#3955=FACE_OUTER_BOUND('',#5315,.T.);
#3956=FACE_OUTER_BOUND('',#5316,.T.);
#3957=FACE_OUTER_BOUND('',#5317,.T.);
#3958=FACE_OUTER_BOUND('',#5318,.T.);
#3959=FACE_OUTER_BOUND('',#5319,.T.);
#3960=FACE_OUTER_BOUND('',#5320,.T.);
#3961=FACE_OUTER_BOUND('',#5321,.T.);
#3962=FACE_OUTER_BOUND('',#5322,.T.);
#3963=FACE_OUTER_BOUND('',#5323,.T.);
#3964=FACE_OUTER_BOUND('',#5324,.T.);
#3965=FACE_OUTER_BOUND('',#5325,.T.);
#3966=FACE_OUTER_BOUND('',#5326,.T.);
#3967=FACE_OUTER_BOUND('',#5327,.T.);
#3968=FACE_OUTER_BOUND('',#5328,.T.);
#3969=FACE_OUTER_BOUND('',#5329,.T.);
#3970=FACE_OUTER_BOUND('',#5330,.T.);
#3971=FACE_OUTER_BOUND('',#5331,.T.);
#3972=FACE_OUTER_BOUND('',#5332,.T.);
#3973=FACE_OUTER_BOUND('',#5333,.T.);
#3974=FACE_OUTER_BOUND('',#5334,.T.);
#3975=FACE_OUTER_BOUND('',#5335,.T.);
#3976=FACE_OUTER_BOUND('',#5336,.T.);
#3977=FACE_OUTER_BOUND('',#5337,.T.);
#3978=FACE_OUTER_BOUND('',#5338,.T.);
#3979=FACE_OUTER_BOUND('',#5339,.T.);
#3980=FACE_OUTER_BOUND('',#5340,.T.);
#3981=FACE_OUTER_BOUND('',#5341,.T.);
#3982=FACE_OUTER_BOUND('',#5342,.T.);
#3983=FACE_OUTER_BOUND('',#5343,.T.);
#3984=FACE_OUTER_BOUND('',#5344,.T.);
#3985=FACE_OUTER_BOUND('',#5345,.T.);
#3986=FACE_OUTER_BOUND('',#5346,.T.);
#3987=FACE_OUTER_BOUND('',#5347,.T.);
#3988=FACE_OUTER_BOUND('',#5348,.T.);
#3989=FACE_OUTER_BOUND('',#5349,.T.);
#3990=FACE_OUTER_BOUND('',#5350,.T.);
#3991=FACE_OUTER_BOUND('',#5351,.T.);
#3992=FACE_OUTER_BOUND('',#5352,.T.);
#3993=FACE_OUTER_BOUND('',#5353,.T.);
#3994=FACE_OUTER_BOUND('',#5354,.T.);
#3995=FACE_OUTER_BOUND('',#5355,.T.);
#3996=FACE_OUTER_BOUND('',#5356,.T.);
#3997=FACE_OUTER_BOUND('',#5357,.T.);
#3998=FACE_OUTER_BOUND('',#5358,.T.);
#3999=FACE_OUTER_BOUND('',#5359,.T.);
#4000=FACE_OUTER_BOUND('',#5360,.T.);
#4001=FACE_OUTER_BOUND('',#5361,.T.);
#4002=FACE_OUTER_BOUND('',#5362,.T.);
#4003=FACE_OUTER_BOUND('',#5363,.T.);
#4004=FACE_OUTER_BOUND('',#5364,.T.);
#4005=FACE_OUTER_BOUND('',#5365,.T.);
#4006=FACE_OUTER_BOUND('',#5366,.T.);
#4007=FACE_OUTER_BOUND('',#5367,.T.);
#4008=FACE_OUTER_BOUND('',#5368,.T.);
#4009=FACE_OUTER_BOUND('',#5369,.T.);
#4010=FACE_OUTER_BOUND('',#5370,.T.);
#4011=FACE_OUTER_BOUND('',#5371,.T.);
#4012=FACE_OUTER_BOUND('',#5372,.T.);
#4013=FACE_OUTER_BOUND('',#5373,.T.);
#4014=FACE_OUTER_BOUND('',#5374,.T.);
#4015=FACE_OUTER_BOUND('',#5375,.T.);
#4016=FACE_OUTER_BOUND('',#5376,.T.);
#4017=FACE_OUTER_BOUND('',#5377,.T.);
#4018=FACE_OUTER_BOUND('',#5378,.T.);
#4019=FACE_OUTER_BOUND('',#5379,.T.);
#4020=FACE_OUTER_BOUND('',#5380,.T.);
#4021=FACE_OUTER_BOUND('',#5381,.T.);
#4022=FACE_OUTER_BOUND('',#5382,.T.);
#4023=FACE_OUTER_BOUND('',#5383,.T.);
#4024=FACE_OUTER_BOUND('',#5384,.T.);
#4025=FACE_OUTER_BOUND('',#5385,.T.);
#4026=FACE_OUTER_BOUND('',#5386,.T.);
#4027=FACE_OUTER_BOUND('',#5387,.T.);
#4028=FACE_OUTER_BOUND('',#5388,.T.);
#4029=FACE_OUTER_BOUND('',#5389,.T.);
#4030=FACE_OUTER_BOUND('',#5390,.T.);
#4031=FACE_OUTER_BOUND('',#5391,.T.);
#4032=FACE_OUTER_BOUND('',#5392,.T.);
#4033=FACE_OUTER_BOUND('',#5393,.T.);
#4034=FACE_OUTER_BOUND('',#5394,.T.);
#4035=FACE_OUTER_BOUND('',#5395,.T.);
#4036=FACE_OUTER_BOUND('',#5396,.T.);
#4037=FACE_OUTER_BOUND('',#5397,.T.);
#4038=FACE_OUTER_BOUND('',#5398,.T.);
#4039=FACE_OUTER_BOUND('',#5399,.T.);
#4040=FACE_OUTER_BOUND('',#5400,.T.);
#4041=FACE_OUTER_BOUND('',#5401,.T.);
#4042=FACE_OUTER_BOUND('',#5402,.T.);
#4043=FACE_OUTER_BOUND('',#5403,.T.);
#4044=FACE_OUTER_BOUND('',#5404,.T.);
#4045=FACE_OUTER_BOUND('',#5405,.T.);
#4046=FACE_OUTER_BOUND('',#5406,.T.);
#4047=FACE_OUTER_BOUND('',#5407,.T.);
#4048=FACE_OUTER_BOUND('',#5408,.T.);
#4049=FACE_OUTER_BOUND('',#5409,.T.);
#4050=FACE_OUTER_BOUND('',#5410,.T.);
#4051=FACE_OUTER_BOUND('',#5411,.T.);
#4052=FACE_OUTER_BOUND('',#5412,.T.);
#4053=FACE_OUTER_BOUND('',#5413,.T.);
#4054=FACE_OUTER_BOUND('',#5414,.T.);
#4055=FACE_OUTER_BOUND('',#5415,.T.);
#4056=FACE_OUTER_BOUND('',#5416,.T.);
#4057=FACE_OUTER_BOUND('',#5417,.T.);
#4058=FACE_OUTER_BOUND('',#5418,.T.);
#4059=FACE_OUTER_BOUND('',#5419,.T.);
#4060=FACE_OUTER_BOUND('',#5420,.T.);
#4061=FACE_OUTER_BOUND('',#5421,.T.);
#4062=FACE_OUTER_BOUND('',#5422,.T.);
#4063=FACE_OUTER_BOUND('',#5423,.T.);
#4064=FACE_OUTER_BOUND('',#5424,.T.);
#4065=FACE_OUTER_BOUND('',#5425,.T.);
#4066=FACE_OUTER_BOUND('',#5426,.T.);
#4067=FACE_OUTER_BOUND('',#5427,.T.);
#4068=FACE_OUTER_BOUND('',#5428,.T.);
#4069=FACE_OUTER_BOUND('',#5429,.T.);
#4070=FACE_OUTER_BOUND('',#5430,.T.);
#4071=FACE_OUTER_BOUND('',#5431,.T.);
#4072=FACE_OUTER_BOUND('',#5432,.T.);
#4073=FACE_OUTER_BOUND('',#5433,.T.);
#4074=FACE_OUTER_BOUND('',#5434,.T.);
#4075=FACE_OUTER_BOUND('',#5435,.T.);
#4076=FACE_OUTER_BOUND('',#5436,.T.);
#4077=FACE_OUTER_BOUND('',#5437,.T.);
#4078=FACE_OUTER_BOUND('',#5438,.T.);
#4079=FACE_OUTER_BOUND('',#5439,.T.);
#4080=FACE_OUTER_BOUND('',#5440,.T.);
#4081=FACE_OUTER_BOUND('',#5441,.T.);
#4082=FACE_OUTER_BOUND('',#5442,.T.);
#4083=FACE_OUTER_BOUND('',#5443,.T.);
#4084=FACE_OUTER_BOUND('',#5444,.T.);
#4085=FACE_OUTER_BOUND('',#5445,.T.);
#4086=FACE_OUTER_BOUND('',#5446,.T.);
#4087=FACE_OUTER_BOUND('',#5447,.T.);
#4088=FACE_OUTER_BOUND('',#5448,.T.);
#4089=FACE_OUTER_BOUND('',#5449,.T.);
#4090=FACE_OUTER_BOUND('',#5450,.T.);
#4091=FACE_OUTER_BOUND('',#5451,.T.);
#4092=FACE_OUTER_BOUND('',#5452,.T.);
#4093=FACE_OUTER_BOUND('',#5453,.T.);
#4094=FACE_OUTER_BOUND('',#5454,.T.);
#4095=FACE_OUTER_BOUND('',#5455,.T.);
#4096=FACE_OUTER_BOUND('',#5456,.T.);
#4097=FACE_OUTER_BOUND('',#5457,.T.);
#4098=FACE_OUTER_BOUND('',#5458,.T.);
#4099=FACE_OUTER_BOUND('',#5459,.T.);
#4100=FACE_OUTER_BOUND('',#5460,.T.);
#4101=FACE_OUTER_BOUND('',#5461,.T.);
#4102=FACE_OUTER_BOUND('',#5462,.T.);
#4103=FACE_OUTER_BOUND('',#5463,.T.);
#4104=FACE_OUTER_BOUND('',#5464,.T.);
#4105=FACE_OUTER_BOUND('',#5465,.T.);
#4106=FACE_OUTER_BOUND('',#5466,.T.);
#4107=FACE_OUTER_BOUND('',#5467,.T.);
#4108=FACE_OUTER_BOUND('',#5468,.T.);
#4109=FACE_OUTER_BOUND('',#5469,.T.);
#4110=FACE_OUTER_BOUND('',#5470,.T.);
#4111=FACE_OUTER_BOUND('',#5471,.T.);
#4112=FACE_OUTER_BOUND('',#5472,.T.);
#4113=FACE_OUTER_BOUND('',#5473,.T.);
#4114=FACE_OUTER_BOUND('',#5474,.T.);
#4115=FACE_OUTER_BOUND('',#5475,.T.);
#4116=FACE_OUTER_BOUND('',#5476,.T.);
#4117=FACE_OUTER_BOUND('',#5477,.T.);
#4118=FACE_OUTER_BOUND('',#5478,.T.);
#4119=FACE_OUTER_BOUND('',#5479,.T.);
#4120=FACE_OUTER_BOUND('',#5480,.T.);
#4121=FACE_OUTER_BOUND('',#5481,.T.);
#4122=FACE_OUTER_BOUND('',#5482,.T.);
#4123=FACE_OUTER_BOUND('',#5483,.T.);
#4124=FACE_OUTER_BOUND('',#5484,.T.);
#4125=FACE_OUTER_BOUND('',#5485,.T.);
#4126=FACE_OUTER_BOUND('',#5486,.T.);
#4127=FACE_OUTER_BOUND('',#5487,.T.);
#4128=FACE_OUTER_BOUND('',#5488,.T.);
#4129=FACE_OUTER_BOUND('',#5489,.T.);
#4130=FACE_OUTER_BOUND('',#5490,.T.);
#4131=FACE_OUTER_BOUND('',#5491,.T.);
#4132=FACE_OUTER_BOUND('',#5492,.T.);
#4133=FACE_OUTER_BOUND('',#5493,.T.);
#4134=FACE_OUTER_BOUND('',#5494,.T.);
#4135=FACE_OUTER_BOUND('',#5495,.T.);
#4136=FACE_OUTER_BOUND('',#5496,.T.);
#4137=FACE_OUTER_BOUND('',#5497,.T.);
#4138=FACE_OUTER_BOUND('',#5498,.T.);
#4139=FACE_OUTER_BOUND('',#5499,.T.);
#4140=FACE_OUTER_BOUND('',#5500,.T.);
#4141=FACE_OUTER_BOUND('',#5501,.T.);
#4142=FACE_OUTER_BOUND('',#5502,.T.);
#4143=FACE_OUTER_BOUND('',#5503,.T.);
#4144=FACE_OUTER_BOUND('',#5504,.T.);
#4145=FACE_OUTER_BOUND('',#5505,.T.);
#4146=FACE_OUTER_BOUND('',#5506,.T.);
#4147=FACE_OUTER_BOUND('',#5507,.T.);
#4148=FACE_OUTER_BOUND('',#5508,.T.);
#4149=FACE_OUTER_BOUND('',#5509,.T.);
#4150=FACE_OUTER_BOUND('',#5510,.T.);
#4151=FACE_OUTER_BOUND('',#5511,.T.);
#4152=FACE_OUTER_BOUND('',#5512,.T.);
#4153=FACE_OUTER_BOUND('',#5513,.T.);
#4154=FACE_OUTER_BOUND('',#5514,.T.);
#4155=FACE_OUTER_BOUND('',#5515,.T.);
#4156=FACE_OUTER_BOUND('',#5516,.T.);
#4157=FACE_OUTER_BOUND('',#5517,.T.);
#4158=FACE_OUTER_BOUND('',#5518,.T.);
#4159=FACE_OUTER_BOUND('',#5519,.T.);
#4160=FACE_OUTER_BOUND('',#5520,.T.);
#4161=FACE_OUTER_BOUND('',#5521,.T.);
#4162=FACE_OUTER_BOUND('',#5522,.T.);
#4163=FACE_OUTER_BOUND('',#5523,.T.);
#4164=FACE_OUTER_BOUND('',#5524,.T.);
#4165=FACE_OUTER_BOUND('',#5525,.T.);
#4166=FACE_OUTER_BOUND('',#5526,.T.);
#4167=FACE_OUTER_BOUND('',#5527,.T.);
#4168=FACE_OUTER_BOUND('',#5528,.T.);
#4169=FACE_OUTER_BOUND('',#5529,.T.);
#4170=FACE_OUTER_BOUND('',#5530,.T.);
#4171=FACE_OUTER_BOUND('',#5531,.T.);
#4172=FACE_OUTER_BOUND('',#5532,.T.);
#4173=FACE_OUTER_BOUND('',#5533,.T.);
#4174=FACE_OUTER_BOUND('',#5534,.T.);
#4175=FACE_OUTER_BOUND('',#5544,.T.);
#4176=FACE_OUTER_BOUND('',#5545,.T.);
#4177=FACE_OUTER_BOUND('',#5546,.T.);
#4178=FACE_OUTER_BOUND('',#5547,.T.);
#4179=FACE_OUTER_BOUND('',#5548,.T.);
#4180=FACE_OUTER_BOUND('',#5549,.T.);
#4181=FACE_OUTER_BOUND('',#5550,.T.);
#4182=FACE_OUTER_BOUND('',#5551,.T.);
#4183=FACE_OUTER_BOUND('',#5552,.T.);
#4184=FACE_OUTER_BOUND('',#5553,.T.);
#4185=FACE_OUTER_BOUND('',#5554,.T.);
#4186=FACE_OUTER_BOUND('',#5555,.T.);
#4187=FACE_OUTER_BOUND('',#5556,.T.);
#4188=FACE_OUTER_BOUND('',#5557,.T.);
#4189=FACE_OUTER_BOUND('',#5558,.T.);
#4190=FACE_OUTER_BOUND('',#5559,.T.);
#4191=FACE_OUTER_BOUND('',#5560,.T.);
#4192=FACE_OUTER_BOUND('',#5561,.T.);
#4193=FACE_OUTER_BOUND('',#5562,.T.);
#4194=FACE_OUTER_BOUND('',#5563,.T.);
#4195=FACE_OUTER_BOUND('',#5564,.T.);
#4196=FACE_OUTER_BOUND('',#5566,.T.);
#4197=FACE_OUTER_BOUND('',#5567,.T.);
#4198=FACE_OUTER_BOUND('',#5568,.T.);
#4199=FACE_OUTER_BOUND('',#5569,.T.);
#4200=FACE_OUTER_BOUND('',#5570,.T.);
#4201=FACE_OUTER_BOUND('',#5571,.T.);
#4202=FACE_OUTER_BOUND('',#5575,.T.);
#4203=FACE_OUTER_BOUND('',#5576,.T.);
#4204=FACE_OUTER_BOUND('',#5577,.T.);
#4205=FACE_OUTER_BOUND('',#5578,.T.);
#4206=FACE_OUTER_BOUND('',#5579,.T.);
#4207=FACE_OUTER_BOUND('',#5580,.T.);
#4208=FACE_OUTER_BOUND('',#5581,.T.);
#4209=FACE_OUTER_BOUND('',#5582,.T.);
#4210=FACE_OUTER_BOUND('',#5583,.T.);
#4211=FACE_OUTER_BOUND('',#5585,.T.);
#4212=FACE_OUTER_BOUND('',#5586,.T.);
#4213=FACE_OUTER_BOUND('',#5587,.T.);
#4214=FACE_OUTER_BOUND('',#5588,.T.);
#4215=FACE_OUTER_BOUND('',#5589,.T.);
#4216=FACE_OUTER_BOUND('',#5590,.T.);
#4217=FACE_OUTER_BOUND('',#5591,.T.);
#4218=FACE_OUTER_BOUND('',#5592,.T.);
#4219=FACE_OUTER_BOUND('',#5593,.T.);
#4220=FACE_OUTER_BOUND('',#5594,.T.);
#4221=FACE_OUTER_BOUND('',#5595,.T.);
#4222=FACE_OUTER_BOUND('',#5596,.T.);
#4223=FACE_OUTER_BOUND('',#5597,.T.);
#4224=FACE_OUTER_BOUND('',#5601,.T.);
#4225=FACE_OUTER_BOUND('',#5602,.T.);
#4226=FACE_OUTER_BOUND('',#5603,.T.);
#4227=FACE_OUTER_BOUND('',#5604,.T.);
#4228=FACE_OUTER_BOUND('',#5605,.T.);
#4229=FACE_OUTER_BOUND('',#5606,.T.);
#4230=FACE_OUTER_BOUND('',#5607,.T.);
#4231=FACE_OUTER_BOUND('',#5608,.T.);
#4232=FACE_OUTER_BOUND('',#5609,.T.);
#4233=FACE_OUTER_BOUND('',#5611,.T.);
#4234=FACE_OUTER_BOUND('',#5612,.T.);
#4235=FACE_OUTER_BOUND('',#5613,.T.);
#4236=FACE_OUTER_BOUND('',#5614,.T.);
#4237=FACE_OUTER_BOUND('',#5615,.T.);
#4238=FACE_OUTER_BOUND('',#5616,.T.);
#4239=FACE_OUTER_BOUND('',#5617,.T.);
#4240=FACE_OUTER_BOUND('',#5618,.T.);
#4241=FACE_OUTER_BOUND('',#5619,.T.);
#4242=FACE_OUTER_BOUND('',#5621,.T.);
#4243=FACE_OUTER_BOUND('',#5622,.T.);
#4244=FACE_OUTER_BOUND('',#5623,.T.);
#4245=FACE_OUTER_BOUND('',#5626,.T.);
#4246=FACE_OUTER_BOUND('',#5627,.T.);
#4247=FACE_OUTER_BOUND('',#5628,.T.);
#4248=FACE_OUTER_BOUND('',#5629,.T.);
#4249=FACE_OUTER_BOUND('',#5630,.T.);
#4250=FACE_OUTER_BOUND('',#5631,.T.);
#4251=FACE_OUTER_BOUND('',#5632,.T.);
#4252=FACE_OUTER_BOUND('',#5633,.T.);
#4253=FACE_OUTER_BOUND('',#5634,.T.);
#4254=FACE_OUTER_BOUND('',#5635,.T.);
#4255=FACE_OUTER_BOUND('',#5636,.T.);
#4256=FACE_OUTER_BOUND('',#5637,.T.);
#4257=FACE_OUTER_BOUND('',#5638,.T.);
#4258=FACE_OUTER_BOUND('',#5639,.T.);
#4259=FACE_OUTER_BOUND('',#5640,.T.);
#4260=FACE_OUTER_BOUND('',#5641,.T.);
#4261=FACE_OUTER_BOUND('',#5642,.T.);
#4262=FACE_OUTER_BOUND('',#5643,.T.);
#4263=FACE_OUTER_BOUND('',#5644,.T.);
#4264=FACE_OUTER_BOUND('',#5645,.T.);
#4265=FACE_OUTER_BOUND('',#5646,.T.);
#4266=FACE_OUTER_BOUND('',#5647,.T.);
#4267=FACE_OUTER_BOUND('',#5650,.T.);
#4268=FACE_OUTER_BOUND('',#5651,.T.);
#4269=FACE_OUTER_BOUND('',#5652,.T.);
#4270=FACE_OUTER_BOUND('',#5653,.T.);
#4271=FACE_OUTER_BOUND('',#5654,.T.);
#4272=FACE_OUTER_BOUND('',#5655,.T.);
#4273=FACE_OUTER_BOUND('',#5656,.T.);
#4274=FACE_OUTER_BOUND('',#5657,.T.);
#4275=FACE_OUTER_BOUND('',#5658,.T.);
#4276=FACE_OUTER_BOUND('',#5659,.T.);
#5277=EDGE_LOOP('',(#23549,#23550,#23551,#23552));
#5278=EDGE_LOOP('',(#23553,#23554,#23555,#23556,#23557,#23558));
#5279=EDGE_LOOP('',(#23559,#23560,#23561,#23562,#23563,#23564));
#5280=EDGE_LOOP('',(#23565,#23566,#23567,#23568,#23569,#23570));
#5281=EDGE_LOOP('',(#23571,#23572,#23573,#23574));
#5282=EDGE_LOOP('',(#23575,#23576,#23577,#23578,#23579,#23580));
#5283=EDGE_LOOP('',(#23581,#23582,#23583,#23584,#23585,#23586));
#5284=EDGE_LOOP('',(#23587,#23588,#23589,#23590,#23591,#23592));
#5285=EDGE_LOOP('',(#23593,#23594,#23595,#23596,#23597,#23598));
#5286=EDGE_LOOP('',(#23599,#23600,#23601,#23602,#23603,#23604));
#5287=EDGE_LOOP('',(#23605,#23606,#23607,#23608,#23609,#23610));
#5288=EDGE_LOOP('',(#23611,#23612,#23613,#23614,#23615,#23616));
#5289=EDGE_LOOP('',(#23617,#23618,#23619,#23620,#23621,#23622));
#5290=EDGE_LOOP('',(#23623,#23624,#23625,#23626,#23627,#23628));
#5291=EDGE_LOOP('',(#23629,#23630,#23631,#23632,#23633,#23634));
#5292=EDGE_LOOP('',(#23635,#23636,#23637,#23638,#23639,#23640));
#5293=EDGE_LOOP('',(#23641,#23642,#23643,#23644,#23645,#23646));
#5294=EDGE_LOOP('',(#23647,#23648,#23649,#23650,#23651,#23652));
#5295=EDGE_LOOP('',(#23653,#23654,#23655,#23656,#23657,#23658));
#5296=EDGE_LOOP('',(#23659,#23660,#23661,#23662,#23663,#23664));
#5297=EDGE_LOOP('',(#23665,#23666,#23667,#23668,#23669,#23670));
#5298=EDGE_LOOP('',(#23671,#23672,#23673,#23674,#23675,#23676));
#5299=EDGE_LOOP('',(#23677,#23678,#23679,#23680,#23681,#23682));
#5300=EDGE_LOOP('',(#23683,#23684,#23685,#23686,#23687,#23688));
#5301=EDGE_LOOP('',(#23689,#23690,#23691,#23692,#23693,#23694));
#5302=EDGE_LOOP('',(#23695,#23696,#23697,#23698,#23699,#23700));
#5303=EDGE_LOOP('',(#23701,#23702,#23703,#23704,#23705,#23706));
#5304=EDGE_LOOP('',(#23707,#23708,#23709,#23710,#23711,#23712));
#5305=EDGE_LOOP('',(#23713,#23714,#23715,#23716,#23717,#23718));
#5306=EDGE_LOOP('',(#23719,#23720,#23721,#23722,#23723,#23724));
#5307=EDGE_LOOP('',(#23725,#23726,#23727,#23728,#23729,#23730));
#5308=EDGE_LOOP('',(#23731,#23732,#23733,#23734,#23735,#23736));
#5309=EDGE_LOOP('',(#23737,#23738,#23739,#23740,#23741,#23742));
#5310=EDGE_LOOP('',(#23743,#23744,#23745,#23746,#23747,#23748));
#5311=EDGE_LOOP('',(#23749,#23750,#23751,#23752,#23753,#23754));
#5312=EDGE_LOOP('',(#23755,#23756,#23757,#23758,#23759,#23760));
#5313=EDGE_LOOP('',(#23761,#23762,#23763,#23764,#23765,#23766));
#5314=EDGE_LOOP('',(#23767,#23768,#23769,#23770,#23771,#23772));
#5315=EDGE_LOOP('',(#23773,#23774,#23775,#23776,#23777,#23778));
#5316=EDGE_LOOP('',(#23779,#23780,#23781,#23782,#23783,#23784));
#5317=EDGE_LOOP('',(#23785,#23786,#23787,#23788,#23789,#23790));
#5318=EDGE_LOOP('',(#23791,#23792,#23793,#23794,#23795,#23796));
#5319=EDGE_LOOP('',(#23797,#23798,#23799,#23800,#23801,#23802));
#5320=EDGE_LOOP('',(#23803,#23804,#23805,#23806,#23807,#23808));
#5321=EDGE_LOOP('',(#23809,#23810,#23811,#23812,#23813,#23814));
#5322=EDGE_LOOP('',(#23815,#23816,#23817,#23818,#23819,#23820));
#5323=EDGE_LOOP('',(#23821,#23822,#23823,#23824,#23825,#23826));
#5324=EDGE_LOOP('',(#23827,#23828,#23829,#23830,#23831,#23832));
#5325=EDGE_LOOP('',(#23833,#23834,#23835,#23836,#23837,#23838));
#5326=EDGE_LOOP('',(#23839,#23840,#23841,#23842,#23843,#23844));
#5327=EDGE_LOOP('',(#23845,#23846,#23847,#23848,#23849,#23850));
#5328=EDGE_LOOP('',(#23851,#23852,#23853,#23854,#23855,#23856));
#5329=EDGE_LOOP('',(#23857,#23858,#23859,#23860,#23861,#23862));
#5330=EDGE_LOOP('',(#23863,#23864,#23865,#23866,#23867,#23868));
#5331=EDGE_LOOP('',(#23869,#23870,#23871,#23872,#23873,#23874));
#5332=EDGE_LOOP('',(#23875,#23876,#23877,#23878,#23879,#23880));
#5333=EDGE_LOOP('',(#23881,#23882,#23883,#23884,#23885,#23886));
#5334=EDGE_LOOP('',(#23887,#23888,#23889,#23890,#23891,#23892));
#5335=EDGE_LOOP('',(#23893,#23894,#23895,#23896,#23897,#23898));
#5336=EDGE_LOOP('',(#23899,#23900,#23901,#23902,#23903,#23904));
#5337=EDGE_LOOP('',(#23905,#23906,#23907,#23908,#23909,#23910));
#5338=EDGE_LOOP('',(#23911,#23912,#23913,#23914,#23915,#23916));
#5339=EDGE_LOOP('',(#23917,#23918,#23919,#23920,#23921,#23922));
#5340=EDGE_LOOP('',(#23923,#23924,#23925,#23926,#23927,#23928));
#5341=EDGE_LOOP('',(#23929,#23930,#23931,#23932,#23933,#23934));
#5342=EDGE_LOOP('',(#23935,#23936,#23937,#23938,#23939,#23940));
#5343=EDGE_LOOP('',(#23941,#23942,#23943,#23944,#23945,#23946));
#5344=EDGE_LOOP('',(#23947,#23948,#23949,#23950,#23951,#23952));
#5345=EDGE_LOOP('',(#23953,#23954,#23955,#23956,#23957,#23958));
#5346=EDGE_LOOP('',(#23959,#23960,#23961,#23962,#23963,#23964));
#5347=EDGE_LOOP('',(#23965,#23966,#23967,#23968,#23969,#23970));
#5348=EDGE_LOOP('',(#23971,#23972,#23973,#23974,#23975,#23976));
#5349=EDGE_LOOP('',(#23977,#23978,#23979,#23980,#23981,#23982));
#5350=EDGE_LOOP('',(#23983,#23984,#23985,#23986,#23987,#23988));
#5351=EDGE_LOOP('',(#23989,#23990,#23991,#23992,#23993,#23994));
#5352=EDGE_LOOP('',(#23995,#23996,#23997,#23998,#23999,#24000));
#5353=EDGE_LOOP('',(#24001,#24002,#24003,#24004,#24005,#24006));
#5354=EDGE_LOOP('',(#24007,#24008,#24009,#24010,#24011,#24012));
#5355=EDGE_LOOP('',(#24013,#24014,#24015,#24016,#24017,#24018));
#5356=EDGE_LOOP('',(#24019,#24020,#24021,#24022,#24023,#24024));
#5357=EDGE_LOOP('',(#24025,#24026,#24027,#24028,#24029,#24030));
#5358=EDGE_LOOP('',(#24031,#24032,#24033,#24034,#24035,#24036));
#5359=EDGE_LOOP('',(#24037,#24038,#24039,#24040,#24041,#24042));
#5360=EDGE_LOOP('',(#24043,#24044,#24045,#24046,#24047,#24048));
#5361=EDGE_LOOP('',(#24049,#24050,#24051,#24052,#24053,#24054));
#5362=EDGE_LOOP('',(#24055,#24056,#24057,#24058,#24059,#24060));
#5363=EDGE_LOOP('',(#24061,#24062,#24063,#24064,#24065,#24066));
#5364=EDGE_LOOP('',(#24067,#24068,#24069,#24070,#24071,#24072));
#5365=EDGE_LOOP('',(#24073,#24074,#24075,#24076,#24077,#24078));
#5366=EDGE_LOOP('',(#24079,#24080,#24081,#24082,#24083,#24084));
#5367=EDGE_LOOP('',(#24085,#24086,#24087,#24088,#24089,#24090));
#5368=EDGE_LOOP('',(#24091,#24092,#24093,#24094,#24095,#24096));
#5369=EDGE_LOOP('',(#24097,#24098,#24099,#24100,#24101,#24102));
#5370=EDGE_LOOP('',(#24103,#24104,#24105,#24106,#24107,#24108));
#5371=EDGE_LOOP('',(#24109,#24110,#24111,#24112,#24113,#24114));
#5372=EDGE_LOOP('',(#24115,#24116,#24117,#24118,#24119,#24120));
#5373=EDGE_LOOP('',(#24121,#24122,#24123,#24124,#24125,#24126));
#5374=EDGE_LOOP('',(#24127,#24128,#24129,#24130,#24131,#24132));
#5375=EDGE_LOOP('',(#24133,#24134,#24135,#24136,#24137,#24138));
#5376=EDGE_LOOP('',(#24139,#24140,#24141,#24142,#24143,#24144));
#5377=EDGE_LOOP('',(#24145,#24146,#24147,#24148,#24149,#24150));
#5378=EDGE_LOOP('',(#24151,#24152,#24153,#24154,#24155,#24156));
#5379=EDGE_LOOP('',(#24157,#24158,#24159,#24160,#24161,#24162));
#5380=EDGE_LOOP('',(#24163,#24164,#24165,#24166,#24167,#24168));
#5381=EDGE_LOOP('',(#24169,#24170,#24171,#24172,#24173,#24174));
#5382=EDGE_LOOP('',(#24175,#24176,#24177,#24178,#24179,#24180));
#5383=EDGE_LOOP('',(#24181,#24182,#24183,#24184,#24185,#24186));
#5384=EDGE_LOOP('',(#24187,#24188,#24189,#24190,#24191,#24192));
#5385=EDGE_LOOP('',(#24193,#24194,#24195,#24196,#24197,#24198));
#5386=EDGE_LOOP('',(#24199,#24200,#24201,#24202,#24203,#24204));
#5387=EDGE_LOOP('',(#24205,#24206,#24207,#24208,#24209,#24210));
#5388=EDGE_LOOP('',(#24211,#24212,#24213,#24214,#24215,#24216));
#5389=EDGE_LOOP('',(#24217,#24218,#24219,#24220,#24221,#24222));
#5390=EDGE_LOOP('',(#24223,#24224,#24225,#24226,#24227,#24228));
#5391=EDGE_LOOP('',(#24229,#24230,#24231,#24232,#24233,#24234));
#5392=EDGE_LOOP('',(#24235,#24236,#24237,#24238,#24239,#24240));
#5393=EDGE_LOOP('',(#24241,#24242,#24243));
#5394=EDGE_LOOP('',(#24244,#24245,#24246,#24247,#24248));
#5395=EDGE_LOOP('',(#24249,#24250,#24251,#24252));
#5396=EDGE_LOOP('',(#24253,#24254,#24255,#24256));
#5397=EDGE_LOOP('',(#24257,#24258,#24259,#24260));
#5398=EDGE_LOOP('',(#24261,#24262,#24263,#24264));
#5399=EDGE_LOOP('',(#24265,#24266,#24267,#24268));
#5400=EDGE_LOOP('',(#24269,#24270,#24271,#24272,#24273));
#5401=EDGE_LOOP('',(#24274,#24275,#24276,#24277,#24278,#24279));
#5402=EDGE_LOOP('',(#24280,#24281,#24282,#24283,#24284));
#5403=EDGE_LOOP('',(#24285,#24286,#24287,#24288,#24289));
#5404=EDGE_LOOP('',(#24290,#24291,#24292,#24293,#24294,#24295));
#5405=EDGE_LOOP('',(#24296,#24297,#24298,#24299));
#5406=EDGE_LOOP('',(#24300,#24301,#24302,#24303,#24304,#24305));
#5407=EDGE_LOOP('',(#24306,#24307,#24308,#24309));
#5408=EDGE_LOOP('',(#24310,#24311,#24312,#24313,#24314,#24315));
#5409=EDGE_LOOP('',(#24316,#24317,#24318,#24319,#24320));
#5410=EDGE_LOOP('',(#24321,#24322,#24323,#24324,#24325,#24326));
#5411=EDGE_LOOP('',(#24327,#24328,#24329,#24330));
#5412=EDGE_LOOP('',(#24331,#24332,#24333,#24334,#24335,#24336));
#5413=EDGE_LOOP('',(#24337,#24338,#24339,#24340,#24341));
#5414=EDGE_LOOP('',(#24342,#24343,#24344,#24345,#24346,#24347));
#5415=EDGE_LOOP('',(#24348,#24349,#24350,#24351,#24352));
#5416=EDGE_LOOP('',(#24353,#24354,#24355,#24356,#24357,#24358));
#5417=EDGE_LOOP('',(#24359,#24360,#24361,#24362));
#5418=EDGE_LOOP('',(#24363,#24364,#24365,#24366,#24367,#24368));
#5419=EDGE_LOOP('',(#24369,#24370,#24371,#24372,#24373));
#5420=EDGE_LOOP('',(#24374,#24375,#24376,#24377,#24378,#24379));
#5421=EDGE_LOOP('',(#24380,#24381,#24382,#24383));
#5422=EDGE_LOOP('',(#24384,#24385,#24386,#24387,#24388,#24389));
#5423=EDGE_LOOP('',(#24390,#24391,#24392,#24393));
#5424=EDGE_LOOP('',(#24394,#24395,#24396,#24397,#24398,#24399));
#5425=EDGE_LOOP('',(#24400,#24401,#24402,#24403,#24404));
#5426=EDGE_LOOP('',(#24405,#24406,#24407,#24408,#24409));
#5427=EDGE_LOOP('',(#24410,#24411,#24412,#24413,#24414,#24415));
#5428=EDGE_LOOP('',(#24416,#24417,#24418,#24419,#24420,#24421));
#5429=EDGE_LOOP('',(#24422,#24423,#24424,#24425,#24426));
#5430=EDGE_LOOP('',(#24427,#24428,#24429,#24430,#24431));
#5431=EDGE_LOOP('',(#24432,#24433,#24434,#24435,#24436,#24437));
#5432=EDGE_LOOP('',(#24438,#24439,#24440,#24441));
#5433=EDGE_LOOP('',(#24442,#24443,#24444,#24445,#24446,#24447));
#5434=EDGE_LOOP('',(#24448,#24449,#24450,#24451));
#5435=EDGE_LOOP('',(#24452,#24453,#24454,#24455,#24456,#24457));
#5436=EDGE_LOOP('',(#24458,#24459,#24460,#24461,#24462));
#5437=EDGE_LOOP('',(#24463,#24464,#24465,#24466,#24467,#24468));
#5438=EDGE_LOOP('',(#24469,#24470,#24471,#24472));
#5439=EDGE_LOOP('',(#24473,#24474,#24475,#24476,#24477,#24478));
#5440=EDGE_LOOP('',(#24479,#24480,#24481,#24482,#24483));
#5441=EDGE_LOOP('',(#24484,#24485,#24486,#24487,#24488,#24489));
#5442=EDGE_LOOP('',(#24490,#24491,#24492,#24493,#24494));
#5443=EDGE_LOOP('',(#24495,#24496,#24497,#24498,#24499,#24500));
#5444=EDGE_LOOP('',(#24501,#24502,#24503,#24504));
#5445=EDGE_LOOP('',(#24505,#24506,#24507,#24508,#24509,#24510));
#5446=EDGE_LOOP('',(#24511,#24512,#24513,#24514,#24515));
#5447=EDGE_LOOP('',(#24516,#24517,#24518,#24519,#24520,#24521));
#5448=EDGE_LOOP('',(#24522,#24523,#24524,#24525));
#5449=EDGE_LOOP('',(#24526,#24527,#24528,#24529,#24530,#24531));
#5450=EDGE_LOOP('',(#24532,#24533,#24534,#24535));
#5451=EDGE_LOOP('',(#24536,#24537,#24538,#24539,#24540,#24541));
#5452=EDGE_LOOP('',(#24542,#24543,#24544,#24545,#24546));
#5453=EDGE_LOOP('',(#24547,#24548,#24549,#24550,#24551));
#5454=EDGE_LOOP('',(#24552,#24553,#24554,#24555,#24556,#24557));
#5455=EDGE_LOOP('',(#24558,#24559,#24560,#24561,#24562,#24563));
#5456=EDGE_LOOP('',(#24564,#24565,#24566,#24567,#24568));
#5457=EDGE_LOOP('',(#24569,#24570,#24571,#24572,#24573));
#5458=EDGE_LOOP('',(#24574,#24575,#24576,#24577,#24578,#24579));
#5459=EDGE_LOOP('',(#24580,#24581,#24582,#24583));
#5460=EDGE_LOOP('',(#24584,#24585,#24586,#24587,#24588,#24589));
#5461=EDGE_LOOP('',(#24590,#24591,#24592,#24593));
#5462=EDGE_LOOP('',(#24594,#24595,#24596,#24597,#24598,#24599));
#5463=EDGE_LOOP('',(#24600,#24601,#24602,#24603,#24604));
#5464=EDGE_LOOP('',(#24605,#24606,#24607,#24608,#24609,#24610));
#5465=EDGE_LOOP('',(#24611,#24612,#24613,#24614));
#5466=EDGE_LOOP('',(#24615,#24616,#24617,#24618,#24619,#24620));
#5467=EDGE_LOOP('',(#24621,#24622,#24623,#24624,#24625));
#5468=EDGE_LOOP('',(#24626,#24627,#24628,#24629,#24630,#24631));
#5469=EDGE_LOOP('',(#24632,#24633,#24634,#24635,#24636));
#5470=EDGE_LOOP('',(#24637,#24638,#24639,#24640,#24641,#24642));
#5471=EDGE_LOOP('',(#24643,#24644,#24645,#24646));
#5472=EDGE_LOOP('',(#24647,#24648,#24649,#24650,#24651,#24652));
#5473=EDGE_LOOP('',(#24653,#24654,#24655,#24656,#24657));
#5474=EDGE_LOOP('',(#24658,#24659,#24660,#24661,#24662,#24663));
#5475=EDGE_LOOP('',(#24664,#24665,#24666,#24667));
#5476=EDGE_LOOP('',(#24668,#24669,#24670,#24671,#24672,#24673));
#5477=EDGE_LOOP('',(#24674,#24675,#24676,#24677));
#5478=EDGE_LOOP('',(#24678,#24679,#24680,#24681,#24682,#24683));
#5479=EDGE_LOOP('',(#24684,#24685,#24686,#24687,#24688));
#5480=EDGE_LOOP('',(#24689,#24690,#24691,#24692,#24693));
#5481=EDGE_LOOP('',(#24694,#24695,#24696,#24697,#24698,#24699));
#5482=EDGE_LOOP('',(#24700,#24701,#24702,#24703,#24704,#24705));
#5483=EDGE_LOOP('',(#24706,#24707,#24708,#24709,#24710));
#5484=EDGE_LOOP('',(#24711,#24712,#24713,#24714,#24715));
#5485=EDGE_LOOP('',(#24716,#24717,#24718,#24719,#24720,#24721));
#5486=EDGE_LOOP('',(#24722,#24723,#24724,#24725));
#5487=EDGE_LOOP('',(#24726,#24727,#24728,#24729,#24730,#24731));
#5488=EDGE_LOOP('',(#24732,#24733,#24734,#24735));
#5489=EDGE_LOOP('',(#24736,#24737,#24738,#24739,#24740,#24741));
#5490=EDGE_LOOP('',(#24742,#24743,#24744,#24745,#24746));
#5491=EDGE_LOOP('',(#24747,#24748,#24749,#24750,#24751,#24752));
#5492=EDGE_LOOP('',(#24753,#24754,#24755,#24756));
#5493=EDGE_LOOP('',(#24757,#24758,#24759,#24760,#24761,#24762));
#5494=EDGE_LOOP('',(#24763,#24764,#24765,#24766,#24767));
#5495=EDGE_LOOP('',(#24768,#24769,#24770,#24771,#24772,#24773));
#5496=EDGE_LOOP('',(#24774,#24775,#24776,#24777,#24778));
#5497=EDGE_LOOP('',(#24779,#24780,#24781,#24782,#24783,#24784));
#5498=EDGE_LOOP('',(#24785,#24786,#24787,#24788));
#5499=EDGE_LOOP('',(#24789,#24790,#24791,#24792,#24793,#24794));
#5500=EDGE_LOOP('',(#24795,#24796,#24797,#24798,#24799));
#5501=EDGE_LOOP('',(#24800,#24801,#24802,#24803,#24804,#24805));
#5502=EDGE_LOOP('',(#24806,#24807,#24808,#24809));
#5503=EDGE_LOOP('',(#24810,#24811,#24812,#24813,#24814,#24815));
#5504=EDGE_LOOP('',(#24816,#24817,#24818,#24819));
#5505=EDGE_LOOP('',(#24820,#24821,#24822,#24823,#24824,#24825));
#5506=EDGE_LOOP('',(#24826,#24827,#24828,#24829,#24830));
#5507=EDGE_LOOP('',(#24831,#24832,#24833,#24834,#24835));
#5508=EDGE_LOOP('',(#24836,#24837,#24838,#24839,#24840,#24841));
#5509=EDGE_LOOP('',(#24842,#24843,#24844,#24845));
#5510=EDGE_LOOP('',(#24846,#24847,#24848,#24849));
#5511=EDGE_LOOP('',(#24850,#24851,#24852,#24853));
#5512=EDGE_LOOP('',(#24854,#24855,#24856,#24857));
#5513=EDGE_LOOP('',(#24858,#24859,#24860));
#5514=EDGE_LOOP('',(#24861,#24862,#24863,#24864));
#5515=EDGE_LOOP('',(#24865,#24866,#24867,#24868,#24869,#24870));
#5516=EDGE_LOOP('',(#24871,#24872,#24873,#24874,#24875,#24876));
#5517=EDGE_LOOP('',(#24877,#24878,#24879,#24880,#24881,#24882));
#5518=EDGE_LOOP('',(#24883,#24884,#24885,#24886,#24887,#24888));
#5519=EDGE_LOOP('',(#24889,#24890,#24891,#24892,#24893,#24894));
#5520=EDGE_LOOP('',(#24895,#24896,#24897,#24898,#24899,#24900));
#5521=EDGE_LOOP('',(#24901,#24902,#24903,#24904));
#5522=EDGE_LOOP('',(#24905));
#5523=EDGE_LOOP('',(#24906,#24907,#24908,#24909));
#5524=EDGE_LOOP('',(#24910,#24911,#24912,#24913,#24914));
#5525=EDGE_LOOP('',(#24915,#24916,#24917,#24918));
#5526=EDGE_LOOP('',(#24919));
#5527=EDGE_LOOP('',(#24920,#24921,#24922,#24923));
#5528=EDGE_LOOP('',(#24924,#24925,#24926,#24927,#24928));
#5529=EDGE_LOOP('',(#24929,#24930,#24931,#24932));
#5530=EDGE_LOOP('',(#24933));
#5531=EDGE_LOOP('',(#24934,#24935,#24936,#24937));
#5532=EDGE_LOOP('',(#24938,#24939,#24940,#24941,#24942,#24943));
#5533=EDGE_LOOP('',(#24944,#24945,#24946,#24947,#24948,#24949,#24950,#24951));
#5534=EDGE_LOOP('',(#24952,#24953,#24954,#24955,#24956,#24957,#24958,#24959,
#24960,#24961,#24962,#24963,#24964,#24965,#24966,#24967,#24968,#24969,#24970,
#24971,#24972,#24973,#24974,#24975,#24976,#24977,#24978,#24979,#24980,#24981,
#24982,#24983));
#5535=EDGE_LOOP('',(#24984));
#5536=EDGE_LOOP('',(#24985));
#5537=EDGE_LOOP('',(#24986,#24987,#24988,#24989));
#5538=EDGE_LOOP('',(#24990,#24991,#24992,#24993));
#5539=EDGE_LOOP('',(#24994,#24995,#24996,#24997));
#5540=EDGE_LOOP('',(#24998,#24999,#25000,#25001));
#5541=EDGE_LOOP('',(#25002));
#5542=EDGE_LOOP('',(#25003));
#5543=EDGE_LOOP('',(#25004));
#5544=EDGE_LOOP('',(#25005,#25006,#25007,#25008,#25009,#25010,#25011,#25012,
#25013,#25014,#25015,#25016,#25017,#25018,#25019,#25020));
#5545=EDGE_LOOP('',(#25021,#25022,#25023,#25024,#25025,#25026,#25027,#25028,
#25029,#25030,#25031,#25032,#25033,#25034,#25035));
#5546=EDGE_LOOP('',(#25036,#25037,#25038,#25039,#25040,#25041,#25042,#25043,
#25044,#25045,#25046,#25047,#25048,#25049,#25050,#25051));
#5547=EDGE_LOOP('',(#25052,#25053,#25054,#25055,#25056,#25057,#25058,#25059,
#25060,#25061,#25062,#25063,#25064,#25065,#25066));
#5548=EDGE_LOOP('',(#25067,#25068,#25069,#25070,#25071,#25072,#25073,#25074,
#25075,#25076,#25077,#25078,#25079,#25080,#25081,#25082,#25083,#25084,#25085,
#25086,#25087,#25088,#25089,#25090,#25091,#25092,#25093,#25094,#25095,#25096,
#25097,#25098,#25099,#25100,#25101,#25102,#25103,#25104,#25105,#25106,#25107,
#25108,#25109,#25110,#25111,#25112,#25113,#25114,#25115,#25116,#25117,#25118,
#25119,#25120,#25121,#25122,#25123,#25124,#25125,#25126,#25127,#25128,#25129,
#25130,#25131,#25132,#25133,#25134,#25135,#25136,#25137,#25138,#25139,#25140,
#25141,#25142,#25143,#25144,#25145,#25146,#25147,#25148,#25149,#25150,#25151,
#25152,#25153,#25154,#25155,#25156,#25157,#25158,#25159,#25160,#25161,#25162,
#25163,#25164,#25165,#25166,#25167,#25168,#25169));
#5549=EDGE_LOOP('',(#25170,#25171,#25172,#25173,#25174,#25175,#25176,#25177,
#25178,#25179,#25180,#25181,#25182,#25183,#25184,#25185,#25186,#25187,#25188,
#25189,#25190,#25191,#25192,#25193,#25194,#25195,#25196,#25197,#25198,#25199,
#25200,#25201,#25202,#25203,#25204,#25205,#25206,#25207,#25208,#25209,#25210,
#25211,#25212,#25213,#25214,#25215,#25216,#25217,#25218,#25219,#25220,#25221,
#25222,#25223,#25224,#25225,#25226,#25227,#25228,#25229,#25230,#25231,#25232,
#25233,#25234,#25235,#25236,#25237,#25238,#25239,#25240,#25241,#25242,#25243,
#25244,#25245,#25246,#25247,#25248,#25249,#25250,#25251,#25252,#25253,#25254,
#25255,#25256,#25257,#25258,#25259,#25260,#25261,#25262,#25263,#25264,#25265,
#25266,#25267,#25268,#25269,#25270,#25271,#25272));
#5550=EDGE_LOOP('',(#25273,#25274,#25275,#25276,#25277,#25278,#25279,#25280,
#25281,#25282,#25283,#25284,#25285,#25286,#25287,#25288,#25289,#25290,#25291,
#25292,#25293,#25294,#25295,#25296,#25297,#25298,#25299,#25300,#25301,#25302,
#25303,#25304,#25305,#25306,#25307,#25308,#25309,#25310,#25311,#25312,#25313,
#25314,#25315,#25316,#25317,#25318,#25319,#25320,#25321,#25322,#25323,#25324,
#25325,#25326,#25327,#25328,#25329,#25330,#25331,#25332,#25333,#25334,#25335,
#25336,#25337,#25338,#25339,#25340,#25341,#25342,#25343,#25344,#25345,#25346,
#25347,#25348,#25349,#25350,#25351,#25352,#25353,#25354,#25355,#25356,#25357,
#25358,#25359,#25360,#25361,#25362,#25363,#25364,#25365,#25366,#25367,#25368,
#25369,#25370,#25371,#25372,#25373,#25374,#25375));
#5551=EDGE_LOOP('',(#25376,#25377,#25378,#25379,#25380,#25381,#25382,#25383,
#25384,#25385,#25386,#25387,#25388,#25389,#25390,#25391,#25392,#25393,#25394,
#25395,#25396,#25397,#25398,#25399,#25400,#25401,#25402,#25403,#25404,#25405,
#25406,#25407,#25408,#25409,#25410,#25411,#25412,#25413,#25414,#25415,#25416,
#25417,#25418,#25419,#25420,#25421,#25422,#25423,#25424,#25425,#25426,#25427,
#25428,#25429,#25430,#25431,#25432,#25433,#25434,#25435,#25436,#25437,#25438,
#25439,#25440,#25441,#25442,#25443,#25444,#25445,#25446,#25447,#25448,#25449,
#25450,#25451,#25452,#25453,#25454,#25455,#25456,#25457,#25458,#25459,#25460,
#25461,#25462,#25463,#25464,#25465,#25466,#25467,#25468,#25469,#25470,#25471,
#25472,#25473,#25474,#25475,#25476,#25477,#25478));
#5552=EDGE_LOOP('',(#25479,#25480,#25481,#25482,#25483,#25484,#25485,#25486,
#25487,#25488,#25489,#25490,#25491,#25492,#25493,#25494,#25495,#25496,#25497,
#25498,#25499,#25500,#25501,#25502,#25503,#25504,#25505,#25506,#25507,#25508,
#25509,#25510,#25511,#25512,#25513,#25514,#25515,#25516,#25517,#25518,#25519,
#25520,#25521,#25522,#25523,#25524,#25525,#25526,#25527,#25528,#25529,#25530,
#25531,#25532,#25533,#25534,#25535,#25536,#25537,#25538,#25539,#25540,#25541,
#25542,#25543,#25544,#25545,#25546,#25547,#25548,#25549,#25550,#25551,#25552,
#25553,#25554,#25555,#25556,#25557,#25558,#25559,#25560,#25561,#25562,#25563,
#25564,#25565,#25566,#25567,#25568,#25569,#25570,#25571,#25572,#25573,#25574,
#25575,#25576,#25577,#25578,#25579,#25580,#25581));
#5553=EDGE_LOOP('',(#25582,#25583,#25584,#25585,#25586,#25587,#25588,#25589,
#25590,#25591,#25592,#25593,#25594,#25595,#25596,#25597,#25598,#25599,#25600,
#25601,#25602,#25603,#25604,#25605,#25606,#25607,#25608,#25609,#25610,#25611,
#25612,#25613,#25614,#25615,#25616,#25617,#25618,#25619,#25620,#25621,#25622,
#25623,#25624,#25625,#25626,#25627,#25628,#25629,#25630,#25631,#25632,#25633,
#25634,#25635,#25636,#25637,#25638,#25639,#25640,#25641,#25642,#25643,#25644,
#25645,#25646,#25647,#25648,#25649,#25650,#25651,#25652,#25653,#25654,#25655,
#25656,#25657,#25658,#25659,#25660,#25661,#25662,#25663,#25664,#25665,#25666,
#25667,#25668,#25669,#25670,#25671,#25672,#25673,#25674,#25675,#25676,#25677,
#25678,#25679,#25680,#25681,#25682,#25683,#25684));
#5554=EDGE_LOOP('',(#25685,#25686,#25687,#25688,#25689,#25690,#25691,#25692,
#25693,#25694,#25695,#25696,#25697,#25698,#25699,#25700,#25701,#25702,#25703,
#25704,#25705,#25706,#25707,#25708,#25709,#25710,#25711,#25712,#25713,#25714,
#25715,#25716,#25717,#25718,#25719,#25720,#25721,#25722,#25723,#25724,#25725,
#25726,#25727,#25728,#25729,#25730,#25731,#25732,#25733,#25734,#25735,#25736,
#25737,#25738,#25739,#25740,#25741,#25742,#25743,#25744,#25745,#25746,#25747,
#25748,#25749,#25750,#25751,#25752,#25753,#25754,#25755,#25756,#25757,#25758,
#25759,#25760,#25761,#25762,#25763,#25764,#25765,#25766,#25767,#25768,#25769,
#25770,#25771,#25772,#25773,#25774,#25775,#25776,#25777,#25778,#25779,#25780,
#25781,#25782,#25783,#25784,#25785,#25786,#25787));
#5555=EDGE_LOOP('',(#25788,#25789,#25790,#25791,#25792,#25793,#25794,#25795,
#25796,#25797,#25798,#25799,#25800,#25801,#25802,#25803,#25804,#25805,#25806,
#25807,#25808,#25809,#25810,#25811,#25812,#25813,#25814,#25815,#25816,#25817,
#25818,#25819,#25820,#25821,#25822,#25823,#25824,#25825,#25826,#25827,#25828,
#25829,#25830,#25831,#25832,#25833,#25834,#25835,#25836,#25837,#25838,#25839,
#25840,#25841,#25842,#25843,#25844,#25845,#25846,#25847,#25848,#25849,#25850,
#25851,#25852,#25853,#25854,#25855,#25856,#25857,#25858,#25859,#25860,#25861,
#25862,#25863,#25864,#25865,#25866,#25867,#25868,#25869,#25870,#25871,#25872,
#25873,#25874,#25875,#25876,#25877,#25878,#25879,#25880,#25881,#25882,#25883,
#25884,#25885,#25886,#25887,#25888,#25889,#25890));
#5556=EDGE_LOOP('',(#25891,#25892,#25893,#25894));
#5557=EDGE_LOOP('',(#25895,#25896,#25897,#25898));
#5558=EDGE_LOOP('',(#25899,#25900,#25901,#25902));
#5559=EDGE_LOOP('',(#25903,#25904,#25905,#25906));
#5560=EDGE_LOOP('',(#25907,#25908,#25909,#25910));
#5561=EDGE_LOOP('',(#25911,#25912,#25913,#25914));
#5562=EDGE_LOOP('',(#25915,#25916,#25917,#25918));
#5563=EDGE_LOOP('',(#25919,#25920,#25921,#25922));
#5564=EDGE_LOOP('',(#25923));
#5565=EDGE_LOOP('',(#25924,#25925,#25926,#25927,#25928,#25929,#25930));
#5566=EDGE_LOOP('',(#25931,#25932,#25933,#25934));
#5567=EDGE_LOOP('',(#25935,#25936,#25937,#25938));
#5568=EDGE_LOOP('',(#25939,#25940,#25941,#25942));
#5569=EDGE_LOOP('',(#25943,#25944,#25945,#25946));
#5570=EDGE_LOOP('',(#25947,#25948,#25949,#25950));
#5571=EDGE_LOOP('',(#25951,#25952,#25953,#25954,#25955,#25956));
#5572=EDGE_LOOP('',(#25957,#25958,#25959,#25960));
#5573=EDGE_LOOP('',(#25961));
#5574=EDGE_LOOP('',(#25962));
#5575=EDGE_LOOP('',(#25963,#25964,#25965,#25966));
#5576=EDGE_LOOP('',(#25967,#25968,#25969,#25970));
#5577=EDGE_LOOP('',(#25971,#25972,#25973,#25974));
#5578=EDGE_LOOP('',(#25975,#25976,#25977,#25978));
#5579=EDGE_LOOP('',(#25979,#25980,#25981,#25982));
#5580=EDGE_LOOP('',(#25983,#25984,#25985,#25986));
#5581=EDGE_LOOP('',(#25987,#25988,#25989,#25990));
#5582=EDGE_LOOP('',(#25991,#25992,#25993,#25994));
#5583=EDGE_LOOP('',(#25995));
#5584=EDGE_LOOP('',(#25996,#25997,#25998,#25999,#26000,#26001,#26002));
#5585=EDGE_LOOP('',(#26003,#26004,#26005,#26006,#26007,#26008,#26009));
#5586=EDGE_LOOP('',(#26010,#26011,#26012,#26013,#26014,#26015,#26016));
#5587=EDGE_LOOP('',(#26017,#26018,#26019,#26020));
#5588=EDGE_LOOP('',(#26021));
#5589=EDGE_LOOP('',(#26022,#26023,#26024,#26025,#26026));
#5590=EDGE_LOOP('',(#26027,#26028,#26029,#26030));
#5591=EDGE_LOOP('',(#26031));
#5592=EDGE_LOOP('',(#26032,#26033,#26034,#26035));
#5593=EDGE_LOOP('',(#26036,#26037,#26038,#26039));
#5594=EDGE_LOOP('',(#26040,#26041,#26042,#26043));
#5595=EDGE_LOOP('',(#26044,#26045,#26046,#26047));
#5596=EDGE_LOOP('',(#26048,#26049,#26050,#26051));
#5597=EDGE_LOOP('',(#26052,#26053,#26054,#26055,#26056,#26057));
#5598=EDGE_LOOP('',(#26058,#26059,#26060,#26061));
#5599=EDGE_LOOP('',(#26062));
#5600=EDGE_LOOP('',(#26063));
#5601=EDGE_LOOP('',(#26064,#26065,#26066,#26067));
#5602=EDGE_LOOP('',(#26068,#26069,#26070,#26071));
#5603=EDGE_LOOP('',(#26072,#26073,#26074,#26075));
#5604=EDGE_LOOP('',(#26076,#26077,#26078,#26079));
#5605=EDGE_LOOP('',(#26080,#26081,#26082,#26083));
#5606=EDGE_LOOP('',(#26084,#26085,#26086,#26087));
#5607=EDGE_LOOP('',(#26088,#26089,#26090,#26091));
#5608=EDGE_LOOP('',(#26092,#26093,#26094,#26095));
#5609=EDGE_LOOP('',(#26096));
#5610=EDGE_LOOP('',(#26097,#26098,#26099,#26100,#26101,#26102,#26103));
#5611=EDGE_LOOP('',(#26104,#26105,#26106,#26107));
#5612=EDGE_LOOP('',(#26108,#26109,#26110,#26111));
#5613=EDGE_LOOP('',(#26112,#26113,#26114,#26115));
#5614=EDGE_LOOP('',(#26116,#26117,#26118,#26119));
#5615=EDGE_LOOP('',(#26120,#26121,#26122,#26123));
#5616=EDGE_LOOP('',(#26124,#26125,#26126,#26127));
#5617=EDGE_LOOP('',(#26128,#26129,#26130,#26131));
#5618=EDGE_LOOP('',(#26132,#26133,#26134,#26135));
#5619=EDGE_LOOP('',(#26136));
#5620=EDGE_LOOP('',(#26137,#26138,#26139,#26140,#26141,#26142,#26143));
#5621=EDGE_LOOP('',(#26144,#26145,#26146,#26147,#26148,#26149,#26150));
#5622=EDGE_LOOP('',(#26151,#26152,#26153,#26154,#26155,#26156,#26157));
#5623=EDGE_LOOP('',(#26158,#26159,#26160,#26161,#26162,#26163,#26164,#26165,
#26166,#26167));
#5624=EDGE_LOOP('',(#26168));
#5625=EDGE_LOOP('',(#26169));
#5626=EDGE_LOOP('',(#26170,#26171,#26172,#26173,#26174));
#5627=EDGE_LOOP('',(#26175,#26176,#26177,#26178));
#5628=EDGE_LOOP('',(#26179));
#5629=EDGE_LOOP('',(#26180,#26181,#26182,#26183));
#5630=EDGE_LOOP('',(#26184));
#5631=EDGE_LOOP('',(#26185,#26186,#26187,#26188));
#5632=EDGE_LOOP('',(#26189));
#5633=EDGE_LOOP('',(#26190,#26191,#26192,#26193));
#5634=EDGE_LOOP('',(#26194));
#5635=EDGE_LOOP('',(#26195,#26196,#26197,#26198));
#5636=EDGE_LOOP('',(#26199,#26200,#26201,#26202));
#5637=EDGE_LOOP('',(#26203,#26204,#26205,#26206));
#5638=EDGE_LOOP('',(#26207,#26208,#26209,#26210));
#5639=EDGE_LOOP('',(#26211,#26212,#26213,#26214));
#5640=EDGE_LOOP('',(#26215,#26216,#26217,#26218));
#5641=EDGE_LOOP('',(#26219,#26220,#26221,#26222));
#5642=EDGE_LOOP('',(#26223,#26224,#26225,#26226));
#5643=EDGE_LOOP('',(#26227,#26228,#26229,#26230));
#5644=EDGE_LOOP('',(#26231,#26232,#26233,#26234));
#5645=EDGE_LOOP('',(#26235,#26236,#26237,#26238));
#5646=EDGE_LOOP('',(#26239,#26240,#26241,#26242));
#5647=EDGE_LOOP('',(#26243,#26244,#26245,#26246,#26247,#26248,#26249,#26250,
#26251,#26252));
#5648=EDGE_LOOP('',(#26253));
#5649=EDGE_LOOP('',(#26254));
#5650=EDGE_LOOP('',(#26255,#26256,#26257,#26258));
#5651=EDGE_LOOP('',(#26259,#26260,#26261,#26262));
#5652=EDGE_LOOP('',(#26263,#26264,#26265,#26266));
#5653=EDGE_LOOP('',(#26267,#26268,#26269,#26270));
#5654=EDGE_LOOP('',(#26271,#26272,#26273,#26274));
#5655=EDGE_LOOP('',(#26275,#26276,#26277,#26278));
#5656=EDGE_LOOP('',(#26279,#26280,#26281,#26282));
#5657=EDGE_LOOP('',(#26283,#26284,#26285,#26286,#26287,#26288));
#5658=EDGE_LOOP('',(#26289,#26290,#26291,#26292));
#5659=EDGE_LOOP('',(#26293,#26294,#26295,#26296,#26297,#26298,#26299,#26300,
#26301,#26302,#26303,#26304,#26305,#26306,#26307,#26308,#26309,#26310,#26311,
#26312,#26313,#26314,#26315,#26316,#26317,#26318));
#5660=EDGE_LOOP('',(#26319,#26320,#26321,#26322));
#5661=EDGE_LOOP('',(#26323,#26324,#26325,#26326));
#5662=EDGE_LOOP('',(#26327,#26328,#26329,#26330));
#5663=EDGE_LOOP('',(#26331,#26332,#26333,#26334));
#6208=CIRCLE('',#29722,5.099);
#6209=CIRCLE('',#29727,5.099);
#6210=CIRCLE('',#29732,2.55999999999999);
#6211=CIRCLE('',#29760,2.56);
#6212=CIRCLE('',#29788,2.56);
#6213=CIRCLE('',#29816,2.56);
#6214=CIRCLE('',#29844,4.263);
#6215=CIRCLE('',#29846,4.263);
#6216=CIRCLE('',#29850,4.263);
#6217=CIRCLE('',#29854,4.263);
#6218=CIRCLE('',#29856,2.117);
#6219=CIRCLE('',#29884,2.117);
#6220=CIRCLE('',#29912,2.117);
#6221=CIRCLE('',#29940,2.117);
#6222=CIRCLE('',#29968,2.117);
#6223=CIRCLE('',#29970,2.117);
#6224=CIRCLE('',#29972,2.117);
#6225=CIRCLE('',#29974,2.117);
#6226=CIRCLE('',#29976,4.263);
#6227=CIRCLE('',#29978,4.263);
#6228=CIRCLE('',#29980,2.56);
#6229=CIRCLE('',#29982,2.56);
#6230=CIRCLE('',#29984,2.56);
#6231=CIRCLE('',#29986,2.55999999999999);
#6232=CIRCLE('',#29988,5.099);
#6233=CIRCLE('',#29990,5.099);
#6234=CIRCLE('',#29992,4.);
#6235=CIRCLE('',#29993,4.);
#6236=CIRCLE('',#29996,4.5);
#6237=CIRCLE('',#29997,4.5);
#6238=CIRCLE('',#29999,3.9914370845599);
#6239=CIRCLE('',#30001,4.);
#6240=CIRCLE('',#30002,4.);
#6241=CIRCLE('',#30005,4.5);
#6242=CIRCLE('',#30006,4.5);
#6243=CIRCLE('',#30008,3.99143708455989);
#6244=CIRCLE('',#30010,5.);
#6245=CIRCLE('',#30011,5.);
#6246=CIRCLE('',#30017,0.190999999999999);
#6247=CIRCLE('',#30018,0.190999999999999);
#6248=CIRCLE('',#30019,0.254);
#6249=CIRCLE('',#30020,5.);
#6250=CIRCLE('',#30021,5.);
#6251=CIRCLE('',#30022,5.);
#6252=CIRCLE('',#30023,5.);
#6253=CIRCLE('',#30024,0.253999999999999);
#6254=CIRCLE('',#30025,0.190999999999999);
#6255=CIRCLE('',#30026,0.191);
#6256=CIRCLE('',#30027,2.5);
#6257=CIRCLE('',#30028,2.5);
#6258=CIRCLE('',#30037,3.);
#6259=CIRCLE('',#30038,3.);
#6260=CIRCLE('',#30041,6.);
#6261=CIRCLE('',#30042,6.);
#6262=CIRCLE('',#30045,6.);
#6263=CIRCLE('',#30046,6.);
#6264=CIRCLE('',#30050,4.);
#6265=CIRCLE('',#30051,5.);
#6266=CIRCLE('',#30060,3.);
#6267=CIRCLE('',#30061,3.);
#6268=CIRCLE('',#30066,4.);
#6269=CIRCLE('',#30070,5.);
#6270=CIRCLE('',#30073,6.);
#6271=CIRCLE('',#30074,6.);
#6272=CIRCLE('',#30077,6.);
#6273=CIRCLE('',#30078,6.);
#6274=CIRCLE('',#30082,4.);
#6275=CIRCLE('',#30083,5.);
#6276=CIRCLE('',#30092,3.);
#6277=CIRCLE('',#30093,3.);
#6278=CIRCLE('',#30103,3.);
#6279=CIRCLE('',#30104,3.);
#6280=CIRCLE('',#30111,5.);
#6281=CIRCLE('',#30114,4.);
#6282=CIRCLE('',#30117,2.5);
#6283=CIRCLE('',#30120,2.5);
#6284=CIRCLE('',#30124,3.99143708455989);
#6285=CIRCLE('',#30126,0.190999999999999);
#6286=CIRCLE('',#30129,0.190999999999999);
#6287=CIRCLE('',#30132,0.254);
#6288=CIRCLE('',#30135,5.);
#6289=CIRCLE('',#30137,5.);
#6290=CIRCLE('',#30140,5.);
#6291=CIRCLE('',#30143,5.);
#6292=CIRCLE('',#30146,0.253999999999999);
#6293=CIRCLE('',#30149,0.190999999999999);
#6294=CIRCLE('',#30152,0.191);
#6295=CIRCLE('',#30155,3.9914370845599);
#7722=LINE('',#128406,#9567);
#7723=LINE('',#128445,#9568);
#7724=LINE('',#128705,#9569);
#7725=LINE('',#129149,#9570);
#7726=LINE('',#129445,#9571);
#7727=LINE('',#129484,#9572);
#7728=LINE('',#129744,#9573);
#7729=LINE('',#130188,#9574);
#7730=LINE('',#130484,#9575);
#7731=LINE('',#130572,#9576);
#7732=LINE('',#130723,#9577);
#7733=LINE('',#131056,#9578);
#7734=LINE('',#131337,#9579);
#7735=LINE('',#131673,#9580);
#7736=LINE('',#131835,#9581);
#7737=LINE('',#132105,#9582);
#7738=LINE('',#132380,#9583);
#7739=LINE('',#132714,#9584);
#7740=LINE('',#132876,#9585);
#7741=LINE('',#133143,#9586);
#7742=LINE('',#133421,#9587);
#7743=LINE('',#133754,#9588);
#7744=LINE('',#133919,#9589);
#7745=LINE('',#134188,#9590);
#7746=LINE('',#134469,#9591);
#7747=LINE('',#134802,#9592);
#7748=LINE('',#134961,#9593);
#7749=LINE('',#135231,#9594);
#7750=LINE('',#135512,#9595);
#7751=LINE('',#135843,#9596);
#7752=LINE('',#136006,#9597);
#7753=LINE('',#136272,#9598);
#7754=LINE('',#136553,#9599);
#7755=LINE('',#136886,#9600);
#7756=LINE('',#137167,#9601);
#7757=LINE('',#137265,#9602);
#7758=LINE('',#137353,#9603);
#7759=LINE('',#137504,#9604);
#7760=LINE('',#137837,#9605);
#7761=LINE('',#138118,#9606);
#7762=LINE('',#138454,#9607);
#7763=LINE('',#138616,#9608);
#7764=LINE('',#138886,#9609);
#7765=LINE('',#139161,#9610);
#7766=LINE('',#139495,#9611);
#7767=LINE('',#139657,#9612);
#7768=LINE('',#139924,#9613);
#7769=LINE('',#140202,#9614);
#7770=LINE('',#140535,#9615);
#7771=LINE('',#140700,#9616);
#7772=LINE('',#140969,#9617);
#7773=LINE('',#141250,#9618);
#7774=LINE('',#141583,#9619);
#7775=LINE('',#141742,#9620);
#7776=LINE('',#142012,#9621);
#7777=LINE('',#142293,#9622);
#7778=LINE('',#142624,#9623);
#7779=LINE('',#142787,#9624);
#7780=LINE('',#143053,#9625);
#7781=LINE('',#143334,#9626);
#7782=LINE('',#143667,#9627);
#7783=LINE('',#143948,#9628);
#7784=LINE('',#144046,#9629);
#7785=LINE('',#144134,#9630);
#7786=LINE('',#144285,#9631);
#7787=LINE('',#144618,#9632);
#7788=LINE('',#144899,#9633);
#7789=LINE('',#145235,#9634);
#7790=LINE('',#145397,#9635);
#7791=LINE('',#145667,#9636);
#7792=LINE('',#145942,#9637);
#7793=LINE('',#146276,#9638);
#7794=LINE('',#146438,#9639);
#7795=LINE('',#146705,#9640);
#7796=LINE('',#146983,#9641);
#7797=LINE('',#147316,#9642);
#7798=LINE('',#147481,#9643);
#7799=LINE('',#147750,#9644);
#7800=LINE('',#148031,#9645);
#7801=LINE('',#148364,#9646);
#7802=LINE('',#148523,#9647);
#7803=LINE('',#148793,#9648);
#7804=LINE('',#149074,#9649);
#7805=LINE('',#149405,#9650);
#7806=LINE('',#149568,#9651);
#7807=LINE('',#149834,#9652);
#7808=LINE('',#150115,#9653);
#7809=LINE('',#150448,#9654);
#7810=LINE('',#150729,#9655);
#7811=LINE('',#150827,#9656);
#7812=LINE('',#150915,#9657);
#7813=LINE('',#151066,#9658);
#7814=LINE('',#151399,#9659);
#7815=LINE('',#151680,#9660);
#7816=LINE('',#152016,#9661);
#7817=LINE('',#152178,#9662);
#7818=LINE('',#152448,#9663);
#7819=LINE('',#152723,#9664);
#7820=LINE('',#153057,#9665);
#7821=LINE('',#153219,#9666);
#7822=LINE('',#153486,#9667);
#7823=LINE('',#153764,#9668);
#7824=LINE('',#154097,#9669);
#7825=LINE('',#154262,#9670);
#7826=LINE('',#154531,#9671);
#7827=LINE('',#154812,#9672);
#7828=LINE('',#155145,#9673);
#7829=LINE('',#155304,#9674);
#7830=LINE('',#155574,#9675);
#7831=LINE('',#155855,#9676);
#7832=LINE('',#156186,#9677);
#7833=LINE('',#156349,#9678);
#7834=LINE('',#156615,#9679);
#7835=LINE('',#156896,#9680);
#7836=LINE('',#157229,#9681);
#7837=LINE('',#157510,#9682);
#7838=LINE('',#157608,#9683);
#7839=LINE('',#157630,#9684);
#7840=LINE('',#157742,#9685);
#7841=LINE('',#158030,#9686);
#7842=LINE('',#158316,#9687);
#7843=LINE('',#158372,#9688);
#7844=LINE('',#158658,#9689);
#7845=LINE('',#158948,#9690);
#7846=LINE('',#159060,#9691);
#7847=LINE('',#159392,#9692);
#7848=LINE('',#159828,#9693);
#7849=LINE('',#160287,#9694);
#7850=LINE('',#160589,#9695);
#7851=LINE('',#161061,#9696);
#7852=LINE('',#161551,#9697);
#7853=LINE('',#162069,#9698);
#7854=LINE('',#162548,#9699);
#7855=LINE('',#162967,#9700);
#7856=LINE('',#163235,#9701);
#7857=LINE('',#163693,#9702);
#7858=LINE('',#164156,#9703);
#7859=LINE('',#164456,#9704);
#7860=LINE('',#164897,#9705);
#7861=LINE('',#165320,#9706);
#7862=LINE('',#165618,#9707);
#7863=LINE('',#166082,#9708);
#7864=LINE('',#166550,#9709);
#7865=LINE('',#166793,#9710);
#7866=LINE('',#167225,#9711);
#7867=LINE('',#167693,#9712);
#7868=LINE('',#168203,#9713);
#7869=LINE('',#168673,#9714);
#7870=LINE('',#169139,#9715);
#7871=LINE('',#169438,#9716);
#7872=LINE('',#169916,#9717);
#7873=LINE('',#170351,#9718);
#7874=LINE('',#170683,#9719);
#7875=LINE('',#171119,#9720);
#7876=LINE('',#171574,#9721);
#7877=LINE('',#171878,#9722);
#7878=LINE('',#172350,#9723);
#7879=LINE('',#172832,#9724);
#7880=LINE('',#173338,#9725);
#7881=LINE('',#173819,#9726);
#7882=LINE('',#174284,#9727);
#7883=LINE('',#174552,#9728);
#7884=LINE('',#175010,#9729);
#7885=LINE('',#175473,#9730);
#7886=LINE('',#175773,#9731);
#7887=LINE('',#176224,#9732);
#7888=LINE('',#176649,#9733);
#7889=LINE('',#176935,#9734);
#7890=LINE('',#177403,#9735);
#7891=LINE('',#177871,#9736);
#7892=LINE('',#178114,#9737);
#7893=LINE('',#178546,#9738);
#7894=LINE('',#179016,#9739);
#7895=LINE('',#179546,#9740);
#7896=LINE('',#180016,#9741);
#7897=LINE('',#180480,#9742);
#7898=LINE('',#180749,#9743);
#7899=LINE('',#181227,#9744);
#7900=LINE('',#181662,#9745);
#7901=LINE('',#181994,#9746);
#7902=LINE('',#182430,#9747);
#7903=LINE('',#182889,#9748);
#7904=LINE('',#183191,#9749);
#7905=LINE('',#183651,#9750);
#7906=LINE('',#184133,#9751);
#7907=LINE('',#184643,#9752);
#7908=LINE('',#185114,#9753);
#7909=LINE('',#185537,#9754);
#7910=LINE('',#185805,#9755);
#7911=LINE('',#186265,#9756);
#7912=LINE('',#186728,#9757);
#7913=LINE('',#187052,#9758);
#7914=LINE('',#187537,#9759);
#7915=LINE('',#187998,#9760);
#7916=LINE('',#188298,#9761);
#7917=LINE('',#188762,#9762);
#7918=LINE('',#189230,#9763);
#7919=LINE('',#189473,#9764);
#7920=LINE('',#189905,#9765);
#7921=LINE('',#190381,#9766);
#7922=LINE('',#190891,#9767);
#7923=LINE('',#191365,#9768);
#7924=LINE('',#191823,#9769);
#7925=LINE('',#192078,#9770);
#7926=LINE('',#192558,#9771);
#7927=LINE('',#192993,#9772);
#7928=LINE('',#193325,#9773);
#7929=LINE('',#193761,#9774);
#7930=LINE('',#194218,#9775);
#7931=LINE('',#194522,#9776);
#7932=LINE('',#194984,#9777);
#7933=LINE('',#195462,#9778);
#7934=LINE('',#195954,#9779);
#7935=LINE('',#196425,#9780);
#7936=LINE('',#196894,#9781);
#7937=LINE('',#197162,#9782);
#7938=LINE('',#197628,#9783);
#7939=LINE('',#198093,#9784);
#7940=LINE('',#198391,#9785);
#7941=LINE('',#198842,#9786);
#7942=LINE('',#199267,#9787);
#7943=LINE('',#199561,#9788);
#7944=LINE('',#200027,#9789);
#7945=LINE('',#200495,#9790);
#7946=LINE('',#200738,#9791);
#7947=LINE('',#201216,#9792);
#7948=LINE('',#201694,#9793);
#7949=LINE('',#202222,#9794);
#7950=LINE('',#202696,#9795);
#7951=LINE('',#203142,#9796);
#7952=LINE('',#203439,#9797);
#7953=LINE('',#203915,#9798);
#7954=LINE('',#206271,#9799);
#7955=LINE('',#206279,#9800);
#7956=LINE('',#206282,#9801);
#7957=LINE('',#206285,#9802);
#7958=LINE('',#206289,#9803);
#7959=LINE('',#206290,#9804);
#7960=LINE('',#206295,#9805);
#7961=LINE('',#206303,#9806);
#7962=LINE('',#206306,#9807);
#7963=LINE('',#206310,#9808);
#7964=LINE('',#206313,#9809);
#7965=LINE('',#206314,#9810);
#7966=LINE('',#206319,#9811);
#7967=LINE('',#206324,#9812);
#7968=LINE('',#206326,#9813);
#7969=LINE('',#206327,#9814);
#7970=LINE('',#206330,#9815);
#7971=LINE('',#206332,#9816);
#7972=LINE('',#206334,#9817);
#7973=LINE('',#206335,#9818);
#7974=LINE('',#206338,#9819);
#7975=LINE('',#206339,#9820);
#7976=LINE('',#206340,#9821);
#7977=LINE('',#206345,#9822);
#7978=LINE('',#206349,#9823);
#7979=LINE('',#206353,#9824);
#7980=LINE('',#206357,#9825);
#7981=LINE('',#206359,#9826);
#7982=LINE('',#206361,#9827);
#7983=LINE('',#206363,#9828);
#7984=LINE('',#206365,#9829);
#7985=LINE('',#206369,#9830);
#7986=LINE('',#206373,#9831);
#7987=LINE('',#206375,#9832);
#7988=LINE('',#206377,#9833);
#7989=LINE('',#206379,#9834);
#7990=LINE('',#206381,#9835);
#7991=LINE('',#206385,#9836);
#7992=LINE('',#206389,#9837);
#7993=LINE('',#206393,#9838);
#7994=LINE('',#206396,#9839);
#7995=LINE('',#215199,#9840);
#7996=LINE('',#215201,#9841);
#7997=LINE('',#215203,#9842);
#7998=LINE('',#215204,#9843);
#7999=LINE('',#215207,#9844);
#8000=LINE('',#215209,#9845);
#8001=LINE('',#215210,#9846);
#8002=LINE('',#215213,#9847);
#8003=LINE('',#215215,#9848);
#8004=LINE('',#215216,#9849);
#8005=LINE('',#215219,#9850);
#8006=LINE('',#215221,#9851);
#8007=LINE('',#215222,#9852);
#8008=LINE('',#215225,#9853);
#8009=LINE('',#215227,#9854);
#8010=LINE('',#215228,#9855);
#8011=LINE('',#215231,#9856);
#8012=LINE('',#215233,#9857);
#8013=LINE('',#215234,#9858);
#8014=LINE('',#215236,#9859);
#8015=LINE('',#215237,#9860);
#8016=LINE('',#215242,#9861);
#8017=LINE('',#215250,#9862);
#8018=LINE('',#215253,#9863);
#8019=LINE('',#215256,#9864);
#8020=LINE('',#215258,#9865);
#8021=LINE('',#215259,#9866);
#8022=LINE('',#215264,#9867);
#8023=LINE('',#215267,#9868);
#8024=LINE('',#215268,#9869);
#8025=LINE('',#215270,#9870);
#8026=LINE('',#215271,#9871);
#8027=LINE('',#215280,#9872);
#8028=LINE('',#215282,#9873);
#8029=LINE('',#215284,#9874);
#8030=LINE('',#215285,#9875);
#8031=LINE('',#215288,#9876);
#8032=LINE('',#215290,#9877);
#8033=LINE('',#215291,#9878);
#8034=LINE('',#215294,#9879);
#8035=LINE('',#215296,#9880);
#8036=LINE('',#215297,#9881);
#8037=LINE('',#215300,#9882);
#8038=LINE('',#215302,#9883);
#8039=LINE('',#215303,#9884);
#8040=LINE('',#215306,#9885);
#8041=LINE('',#215308,#9886);
#8042=LINE('',#215309,#9887);
#8043=LINE('',#215312,#9888);
#8044=LINE('',#215314,#9889);
#8045=LINE('',#215315,#9890);
#8046=LINE('',#215317,#9891);
#8047=LINE('',#215318,#9892);
#8048=LINE('',#215323,#9893);
#8049=LINE('',#215330,#9894);
#8050=LINE('',#215336,#9895);
#8051=LINE('',#215344,#9896);
#8052=LINE('',#215347,#9897);
#8053=LINE('',#215350,#9898);
#8054=LINE('',#215352,#9899);
#8055=LINE('',#215353,#9900);
#8056=LINE('',#215359,#9901);
#8057=LINE('',#215361,#9902);
#8058=LINE('',#215362,#9903);
#8059=LINE('',#215364,#9904);
#8060=LINE('',#215365,#9905);
#8061=LINE('',#215374,#9906);
#8062=LINE('',#215376,#9907);
#8063=LINE('',#215378,#9908);
#8064=LINE('',#215379,#9909);
#8065=LINE('',#215382,#9910);
#8066=LINE('',#215384,#9911);
#8067=LINE('',#215385,#9912);
#8068=LINE('',#215388,#9913);
#8069=LINE('',#215390,#9914);
#8070=LINE('',#215391,#9915);
#8071=LINE('',#215394,#9916);
#8072=LINE('',#215396,#9917);
#8073=LINE('',#215397,#9918);
#8074=LINE('',#215400,#9919);
#8075=LINE('',#215402,#9920);
#8076=LINE('',#215403,#9921);
#8077=LINE('',#215406,#9922);
#8078=LINE('',#215408,#9923);
#8079=LINE('',#215409,#9924);
#8080=LINE('',#215411,#9925);
#8081=LINE('',#215412,#9926);
#8082=LINE('',#215417,#9927);
#8083=LINE('',#215423,#9928);
#8084=LINE('',#215425,#9929);
#8085=LINE('',#215427,#9930);
#8086=LINE('',#215428,#9931);
#8087=LINE('',#215431,#9932);
#8088=LINE('',#215433,#9933);
#8089=LINE('',#215434,#9934);
#8090=LINE('',#215437,#9935);
#8091=LINE('',#215439,#9936);
#8092=LINE('',#215440,#9937);
#8093=LINE('',#215443,#9938);
#8094=LINE('',#215445,#9939);
#8095=LINE('',#215446,#9940);
#8096=LINE('',#215449,#9941);
#8097=LINE('',#215451,#9942);
#8098=LINE('',#215452,#9943);
#8099=LINE('',#215455,#9944);
#8100=LINE('',#215457,#9945);
#8101=LINE('',#215458,#9946);
#8102=LINE('',#215460,#9947);
#8103=LINE('',#215461,#9948);
#8104=LINE('',#215466,#9949);
#8105=LINE('',#215473,#9950);
#8106=LINE('',#215475,#9951);
#8107=LINE('',#215476,#9952);
#8108=LINE('',#215481,#9953);
#8109=LINE('',#215486,#9954);
#8110=LINE('',#215491,#9955);
#8111=LINE('',#215496,#9956);
#8112=LINE('',#215500,#9957);
#8113=LINE('',#215501,#9958);
#8114=LINE('',#215507,#9959);
#8115=LINE('',#215510,#9960);
#8116=LINE('',#215511,#9961);
#8117=LINE('',#215515,#9962);
#8118=LINE('',#215518,#9963);
#8119=LINE('',#215519,#9964);
#8120=LINE('',#215523,#9965);
#8121=LINE('',#215526,#9966);
#8122=LINE('',#215527,#9967);
#8123=LINE('',#215533,#9968);
#8124=LINE('',#215536,#9969);
#8125=LINE('',#215537,#9970);
#8126=LINE('',#215541,#9971);
#8127=LINE('',#215544,#9972);
#8128=LINE('',#215545,#9973);
#8129=LINE('',#215549,#9974);
#8130=LINE('',#215552,#9975);
#8131=LINE('',#215553,#9976);
#8132=LINE('',#215557,#9977);
#8133=LINE('',#215560,#9978);
#8134=LINE('',#215561,#9979);
#8135=LINE('',#215565,#9980);
#8136=LINE('',#215568,#9981);
#8137=LINE('',#215569,#9982);
#8138=LINE('',#215573,#9983);
#8139=LINE('',#215576,#9984);
#8140=LINE('',#215577,#9985);
#9567=VECTOR('',#34678,5.099);
#9568=VECTOR('',#34683,5.099);
#9569=VECTOR('',#34686,5.099);
#9570=VECTOR('',#34689,5.099);
#9571=VECTOR('',#34692,5.099);
#9572=VECTOR('',#34697,5.099);
#9573=VECTOR('',#34700,5.099);
#9574=VECTOR('',#34703,5.099);
#9575=VECTOR('',#34706,2.55999999999999);
#9576=VECTOR('',#34711,2.55999999999999);
#9577=VECTOR('',#34714,2.55999999999999);
#9578=VECTOR('',#34717,2.55999999999999);
#9579=VECTOR('',#34720,2.55999999999999);
#9580=VECTOR('',#34723,2.55999999999999);
#9581=VECTOR('',#34726,2.55999999999999);
#9582=VECTOR('',#34729,2.55999999999999);
#9583=VECTOR('',#34732,2.55999999999999);
#9584=VECTOR('',#34735,2.55999999999999);
#9585=VECTOR('',#34738,2.55999999999999);
#9586=VECTOR('',#34741,2.55999999999999);
#9587=VECTOR('',#34744,2.55999999999999);
#9588=VECTOR('',#34747,2.55999999999999);
#9589=VECTOR('',#34750,2.55999999999999);
#9590=VECTOR('',#34753,2.55999999999999);
#9591=VECTOR('',#34756,2.55999999999999);
#9592=VECTOR('',#34759,2.55999999999999);
#9593=VECTOR('',#34762,2.55999999999999);
#9594=VECTOR('',#34765,2.55999999999999);
#9595=VECTOR('',#34768,2.55999999999999);
#9596=VECTOR('',#34771,2.55999999999999);
#9597=VECTOR('',#34774,2.55999999999999);
#9598=VECTOR('',#34777,2.55999999999999);
#9599=VECTOR('',#34780,2.55999999999999);
#9600=VECTOR('',#34783,2.55999999999999);
#9601=VECTOR('',#34786,2.55999999999999);
#9602=VECTOR('',#34789,2.56);
#9603=VECTOR('',#34794,2.56);
#9604=VECTOR('',#34797,2.56);
#9605=VECTOR('',#34800,2.56);
#9606=VECTOR('',#34803,2.56);
#9607=VECTOR('',#34806,2.56);
#9608=VECTOR('',#34809,2.56);
#9609=VECTOR('',#34812,2.56);
#9610=VECTOR('',#34815,2.56);
#9611=VECTOR('',#34818,2.56);
#9612=VECTOR('',#34821,2.56);
#9613=VECTOR('',#34824,2.56);
#9614=VECTOR('',#34827,2.56);
#9615=VECTOR('',#34830,2.56);
#9616=VECTOR('',#34833,2.56);
#9617=VECTOR('',#34836,2.56);
#9618=VECTOR('',#34839,2.56);
#9619=VECTOR('',#34842,2.56);
#9620=VECTOR('',#34845,2.56);
#9621=VECTOR('',#34848,2.56);
#9622=VECTOR('',#34851,2.56);
#9623=VECTOR('',#34854,2.56);
#9624=VECTOR('',#34857,2.56);
#9625=VECTOR('',#34860,2.56);
#9626=VECTOR('',#34863,2.56);
#9627=VECTOR('',#34866,2.56);
#9628=VECTOR('',#34869,2.56);
#9629=VECTOR('',#34872,2.56);
#9630=VECTOR('',#34877,2.56);
#9631=VECTOR('',#34880,2.56);
#9632=VECTOR('',#34883,2.56);
#9633=VECTOR('',#34886,2.56);
#9634=VECTOR('',#34889,2.56);
#9635=VECTOR('',#34892,2.56);
#9636=VECTOR('',#34895,2.56);
#9637=VECTOR('',#34898,2.56);
#9638=VECTOR('',#34901,2.56);
#9639=VECTOR('',#34904,2.56);
#9640=VECTOR('',#34907,2.56);
#9641=VECTOR('',#34910,2.56);
#9642=VECTOR('',#34913,2.56);
#9643=VECTOR('',#34916,2.56);
#9644=VECTOR('',#34919,2.56);
#9645=VECTOR('',#34922,2.56);
#9646=VECTOR('',#34925,2.56);
#9647=VECTOR('',#34928,2.56);
#9648=VECTOR('',#34931,2.56);
#9649=VECTOR('',#34934,2.56);
#9650=VECTOR('',#34937,2.56);
#9651=VECTOR('',#34940,2.56);
#9652=VECTOR('',#34943,2.56);
#9653=VECTOR('',#34946,2.56);
#9654=VECTOR('',#34949,2.56);
#9655=VECTOR('',#34952,2.56);
#9656=VECTOR('',#34955,2.56);
#9657=VECTOR('',#34960,2.56);
#9658=VECTOR('',#34963,2.56);
#9659=VECTOR('',#34966,2.56);
#9660=VECTOR('',#34969,2.56);
#9661=VECTOR('',#34972,2.56);
#9662=VECTOR('',#34975,2.56);
#9663=VECTOR('',#34978,2.56);
#9664=VECTOR('',#34981,2.56);
#9665=VECTOR('',#34984,2.56);
#9666=VECTOR('',#34987,2.56);
#9667=VECTOR('',#34990,2.56);
#9668=VECTOR('',#34993,2.56);
#9669=VECTOR('',#34996,2.56);
#9670=VECTOR('',#34999,2.56);
#9671=VECTOR('',#35002,2.56);
#9672=VECTOR('',#35005,2.56);
#9673=VECTOR('',#35008,2.56);
#9674=VECTOR('',#35011,2.56);
#9675=VECTOR('',#35014,2.56);
#9676=VECTOR('',#35017,2.56);
#9677=VECTOR('',#35020,2.56);
#9678=VECTOR('',#35023,2.56);
#9679=VECTOR('',#35026,2.56);
#9680=VECTOR('',#35029,2.56);
#9681=VECTOR('',#35032,2.56);
#9682=VECTOR('',#35035,2.56);
#9683=VECTOR('',#35038,4.263);
#9684=VECTOR('',#35043,4.263);
#9685=VECTOR('',#35048,4.263);
#9686=VECTOR('',#35051,4.263);
#9687=VECTOR('',#35054,4.263);
#9688=VECTOR('',#35059,4.263);
#9689=VECTOR('',#35062,4.263);
#9690=VECTOR('',#35065,4.263);
#9691=VECTOR('',#35070,2.117);
#9692=VECTOR('',#35075,2.117);
#9693=VECTOR('',#35078,2.117);
#9694=VECTOR('',#35081,2.117);
#9695=VECTOR('',#35084,2.117);
#9696=VECTOR('',#35087,2.117);
#9697=VECTOR('',#35090,2.117);
#9698=VECTOR('',#35093,2.117);
#9699=VECTOR('',#35096,2.117);
#9700=VECTOR('',#35099,2.117);
#9701=VECTOR('',#35102,2.117);
#9702=VECTOR('',#35105,2.117);
#9703=VECTOR('',#35108,2.117);
#9704=VECTOR('',#35111,2.117);
#9705=VECTOR('',#35114,2.117);
#9706=VECTOR('',#35117,2.117);
#9707=VECTOR('',#35120,2.117);
#9708=VECTOR('',#35123,2.117);
#9709=VECTOR('',#35126,2.117);
#9710=VECTOR('',#35129,2.117);
#9711=VECTOR('',#35132,2.117);
#9712=VECTOR('',#35135,2.117);
#9713=VECTOR('',#35138,2.117);
#9714=VECTOR('',#35141,2.117);
#9715=VECTOR('',#35144,2.117);
#9716=VECTOR('',#35147,2.117);
#9717=VECTOR('',#35150,2.117);
#9718=VECTOR('',#35153,2.117);
#9719=VECTOR('',#35158,2.117);
#9720=VECTOR('',#35161,2.117);
#9721=VECTOR('',#35164,2.117);
#9722=VECTOR('',#35167,2.117);
#9723=VECTOR('',#35170,2.117);
#9724=VECTOR('',#35173,2.117);
#9725=VECTOR('',#35176,2.117);
#9726=VECTOR('',#35179,2.117);
#9727=VECTOR('',#35182,2.117);
#9728=VECTOR('',#35185,2.117);
#9729=VECTOR('',#35188,2.117);
#9730=VECTOR('',#35191,2.117);
#9731=VECTOR('',#35194,2.117);
#9732=VECTOR('',#35197,2.117);
#9733=VECTOR('',#35200,2.117);
#9734=VECTOR('',#35203,2.117);
#9735=VECTOR('',#35206,2.117);
#9736=VECTOR('',#35209,2.117);
#9737=VECTOR('',#35212,2.117);
#9738=VECTOR('',#35215,2.117);
#9739=VECTOR('',#35218,2.117);
#9740=VECTOR('',#35221,2.117);
#9741=VECTOR('',#35224,2.117);
#9742=VECTOR('',#35227,2.117);
#9743=VECTOR('',#35230,2.117);
#9744=VECTOR('',#35233,2.117);
#9745=VECTOR('',#35236,2.117);
#9746=VECTOR('',#35241,2.117);
#9747=VECTOR('',#35244,2.117);
#9748=VECTOR('',#35247,2.117);
#9749=VECTOR('',#35250,2.117);
#9750=VECTOR('',#35253,2.117);
#9751=VECTOR('',#35256,2.117);
#9752=VECTOR('',#35259,2.117);
#9753=VECTOR('',#35262,2.117);
#9754=VECTOR('',#35265,2.117);
#9755=VECTOR('',#35268,2.117);
#9756=VECTOR('',#35271,2.117);
#9757=VECTOR('',#35274,2.117);
#9758=VECTOR('',#35277,2.117);
#9759=VECTOR('',#35280,2.117);
#9760=VECTOR('',#35283,2.117);
#9761=VECTOR('',#35286,2.117);
#9762=VECTOR('',#35289,2.117);
#9763=VECTOR('',#35292,2.117);
#9764=VECTOR('',#35295,2.117);
#9765=VECTOR('',#35298,2.117);
#9766=VECTOR('',#35301,2.117);
#9767=VECTOR('',#35304,2.117);
#9768=VECTOR('',#35307,2.117);
#9769=VECTOR('',#35310,2.117);
#9770=VECTOR('',#35313,2.117);
#9771=VECTOR('',#35316,2.117);
#9772=VECTOR('',#35319,2.117);
#9773=VECTOR('',#35324,2.117);
#9774=VECTOR('',#35327,2.117);
#9775=VECTOR('',#35330,2.117);
#9776=VECTOR('',#35333,2.117);
#9777=VECTOR('',#35336,2.117);
#9778=VECTOR('',#35339,2.117);
#9779=VECTOR('',#35342,2.117);
#9780=VECTOR('',#35345,2.117);
#9781=VECTOR('',#35348,2.117);
#9782=VECTOR('',#35351,2.117);
#9783=VECTOR('',#35354,2.117);
#9784=VECTOR('',#35357,2.117);
#9785=VECTOR('',#35360,2.117);
#9786=VECTOR('',#35363,2.117);
#9787=VECTOR('',#35366,2.117);
#9788=VECTOR('',#35369,2.117);
#9789=VECTOR('',#35372,2.117);
#9790=VECTOR('',#35375,2.117);
#9791=VECTOR('',#35378,2.117);
#9792=VECTOR('',#35381,2.117);
#9793=VECTOR('',#35384,2.117);
#9794=VECTOR('',#35387,2.117);
#9795=VECTOR('',#35390,2.117);
#9796=VECTOR('',#35393,2.117);
#9797=VECTOR('',#35396,2.117);
#9798=VECTOR('',#35399,2.117);
#9799=VECTOR('',#35452,4.);
#9800=VECTOR('',#35461,10.);
#9801=VECTOR('',#35464,10.);
#9802=VECTOR('',#35467,10.);
#9803=VECTOR('',#35470,10.);
#9804=VECTOR('',#35471,10.);
#9805=VECTOR('',#35476,4.);
#9806=VECTOR('',#35485,10.);
#9807=VECTOR('',#35488,10.);
#9808=VECTOR('',#35491,10.);
#9809=VECTOR('',#35494,10.);
#9810=VECTOR('',#35495,10.);
#9811=VECTOR('',#35500,5.);
#9812=VECTOR('',#35507,10.);
#9813=VECTOR('',#35508,10.);
#9814=VECTOR('',#35509,10.);
#9815=VECTOR('',#35512,10.);
#9816=VECTOR('',#35513,10.);
#9817=VECTOR('',#35514,10.);
#9818=VECTOR('',#35515,10.);
#9819=VECTOR('',#35518,10.);
#9820=VECTOR('',#35519,10.);
#9821=VECTOR('',#35520,10.);
#9822=VECTOR('',#35525,10.);
#9823=VECTOR('',#35528,10.);
#9824=VECTOR('',#35531,10.);
#9825=VECTOR('',#35534,10.);
#9826=VECTOR('',#35535,10.);
#9827=VECTOR('',#35536,10.);
#9828=VECTOR('',#35537,10.);
#9829=VECTOR('',#35538,10.);
#9830=VECTOR('',#35541,10.);
#9831=VECTOR('',#35544,10.);
#9832=VECTOR('',#35545,10.);
#9833=VECTOR('',#35546,10.);
#9834=VECTOR('',#35547,10.);
#9835=VECTOR('',#35548,10.);
#9836=VECTOR('',#35551,10.);
#9837=VECTOR('',#35554,10.);
#9838=VECTOR('',#35557,10.);
#9839=VECTOR('',#35560,10.);
#9840=VECTOR('',#35567,10.);
#9841=VECTOR('',#35568,10.);
#9842=VECTOR('',#35569,10.);
#9843=VECTOR('',#35570,10.);
#9844=VECTOR('',#35573,10.);
#9845=VECTOR('',#35574,10.);
#9846=VECTOR('',#35575,10.);
#9847=VECTOR('',#35578,10.);
#9848=VECTOR('',#35579,10.);
#9849=VECTOR('',#35580,10.);
#9850=VECTOR('',#35583,10.);
#9851=VECTOR('',#35584,10.);
#9852=VECTOR('',#35585,10.);
#9853=VECTOR('',#35588,10.);
#9854=VECTOR('',#35589,10.);
#9855=VECTOR('',#35590,10.);
#9856=VECTOR('',#35593,10.);
#9857=VECTOR('',#35594,10.);
#9858=VECTOR('',#35595,10.);
#9859=VECTOR('',#35598,10.);
#9860=VECTOR('',#35599,10.);
#9861=VECTOR('',#35604,3.);
#9862=VECTOR('',#35613,10.);
#9863=VECTOR('',#35616,10.);
#9864=VECTOR('',#35619,10.);
#9865=VECTOR('',#35620,10.);
#9866=VECTOR('',#35621,10.);
#9867=VECTOR('',#35626,10.);
#9868=VECTOR('',#35631,10.);
#9869=VECTOR('',#35632,10.);
#9870=VECTOR('',#35635,10.);
#9871=VECTOR('',#35636,10.);
#9872=VECTOR('',#35645,10.);
#9873=VECTOR('',#35646,10.);
#9874=VECTOR('',#35647,10.);
#9875=VECTOR('',#35648,10.);
#9876=VECTOR('',#35651,10.);
#9877=VECTOR('',#35652,10.);
#9878=VECTOR('',#35653,10.);
#9879=VECTOR('',#35656,10.);
#9880=VECTOR('',#35657,10.);
#9881=VECTOR('',#35658,10.);
#9882=VECTOR('',#35661,10.);
#9883=VECTOR('',#35662,10.);
#9884=VECTOR('',#35663,10.);
#9885=VECTOR('',#35666,10.);
#9886=VECTOR('',#35667,10.);
#9887=VECTOR('',#35668,10.);
#9888=VECTOR('',#35671,10.);
#9889=VECTOR('',#35672,10.);
#9890=VECTOR('',#35673,10.);
#9891=VECTOR('',#35676,10.);
#9892=VECTOR('',#35677,10.);
#9893=VECTOR('',#35682,3.);
#9894=VECTOR('',#35693,4.);
#9895=VECTOR('',#35702,5.);
#9896=VECTOR('',#35711,10.);
#9897=VECTOR('',#35714,10.);
#9898=VECTOR('',#35717,10.);
#9899=VECTOR('',#35718,10.);
#9900=VECTOR('',#35719,10.);
#9901=VECTOR('',#35726,10.);
#9902=VECTOR('',#35729,10.);
#9903=VECTOR('',#35730,10.);
#9904=VECTOR('',#35733,10.);
#9905=VECTOR('',#35734,10.);
#9906=VECTOR('',#35743,10.);
#9907=VECTOR('',#35744,10.);
#9908=VECTOR('',#35745,10.);
#9909=VECTOR('',#35746,10.);
#9910=VECTOR('',#35749,10.);
#9911=VECTOR('',#35750,10.);
#9912=VECTOR('',#35751,10.);
#9913=VECTOR('',#35754,10.);
#9914=VECTOR('',#35755,10.);
#9915=VECTOR('',#35756,10.);
#9916=VECTOR('',#35759,10.);
#9917=VECTOR('',#35760,10.);
#9918=VECTOR('',#35761,10.);
#9919=VECTOR('',#35764,10.);
#9920=VECTOR('',#35765,10.);
#9921=VECTOR('',#35766,10.);
#9922=VECTOR('',#35769,10.);
#9923=VECTOR('',#35770,10.);
#9924=VECTOR('',#35771,10.);
#9925=VECTOR('',#35774,10.);
#9926=VECTOR('',#35775,10.);
#9927=VECTOR('',#35780,3.);
#9928=VECTOR('',#35787,10.);
#9929=VECTOR('',#35788,10.);
#9930=VECTOR('',#35789,10.);
#9931=VECTOR('',#35790,10.);
#9932=VECTOR('',#35793,10.);
#9933=VECTOR('',#35794,10.);
#9934=VECTOR('',#35795,10.);
#9935=VECTOR('',#35798,10.);
#9936=VECTOR('',#35799,10.);
#9937=VECTOR('',#35800,10.);
#9938=VECTOR('',#35803,10.);
#9939=VECTOR('',#35804,10.);
#9940=VECTOR('',#35805,10.);
#9941=VECTOR('',#35808,10.);
#9942=VECTOR('',#35809,10.);
#9943=VECTOR('',#35810,10.);
#9944=VECTOR('',#35813,10.);
#9945=VECTOR('',#35814,10.);
#9946=VECTOR('',#35815,10.);
#9947=VECTOR('',#35818,10.);
#9948=VECTOR('',#35819,10.);
#9949=VECTOR('',#35824,3.);
#9950=VECTOR('',#35835,10.);
#9951=VECTOR('',#35836,10.);
#9952=VECTOR('',#35837,10.);
#9953=VECTOR('',#35844,5.);
#9954=VECTOR('',#35851,4.);
#9955=VECTOR('',#35858,2.5);
#9956=VECTOR('',#35865,2.5);
#9957=VECTOR('',#35870,10.);
#9958=VECTOR('',#35871,10.);
#9959=VECTOR('',#35880,10.);
#9960=VECTOR('',#35883,10.);
#9961=VECTOR('',#35884,10.);
#9962=VECTOR('',#35889,10.);
#9963=VECTOR('',#35892,10.);
#9964=VECTOR('',#35893,10.);
#9965=VECTOR('',#35898,10.);
#9966=VECTOR('',#35901,10.);
#9967=VECTOR('',#35902,10.);
#9968=VECTOR('',#35911,10.);
#9969=VECTOR('',#35914,10.);
#9970=VECTOR('',#35915,10.);
#9971=VECTOR('',#35920,10.);
#9972=VECTOR('',#35923,10.);
#9973=VECTOR('',#35924,10.);
#9974=VECTOR('',#35929,10.);
#9975=VECTOR('',#35932,10.);
#9976=VECTOR('',#35933,10.);
#9977=VECTOR('',#35938,10.);
#9978=VECTOR('',#35941,10.);
#9979=VECTOR('',#35942,10.);
#9980=VECTOR('',#35947,10.);
#9981=VECTOR('',#35950,10.);
#9982=VECTOR('',#35951,10.);
#9983=VECTOR('',#35956,10.);
#9984=VECTOR('',#35959,10.);
#9985=VECTOR('',#35960,10.);
#12072=VERTEX_POINT('',#128404);
#12073=VERTEX_POINT('',#128405);
#12074=VERTEX_POINT('',#128407);
#12075=VERTEX_POINT('',#128436);
#12076=VERTEX_POINT('',#128443);
#12077=VERTEX_POINT('',#128444);
#12078=VERTEX_POINT('',#128446);
#12079=VERTEX_POINT('',#128502);
#12080=VERTEX_POINT('',#128703);
#12081=VERTEX_POINT('',#128704);
#12082=VERTEX_POINT('',#128706);
#12083=VERTEX_POINT('',#128906);
#12084=VERTEX_POINT('',#129147);
#12085=VERTEX_POINT('',#129148);
#12086=VERTEX_POINT('',#129150);
#12087=VERTEX_POINT('',#129387);
#12088=VERTEX_POINT('',#129443);
#12089=VERTEX_POINT('',#129444);
#12090=VERTEX_POINT('',#129446);
#12091=VERTEX_POINT('',#129475);
#12092=VERTEX_POINT('',#129482);
#12093=VERTEX_POINT('',#129483);
#12094=VERTEX_POINT('',#129485);
#12095=VERTEX_POINT('',#129541);
#12096=VERTEX_POINT('',#129742);
#12097=VERTEX_POINT('',#129743);
#12098=VERTEX_POINT('',#129745);
#12099=VERTEX_POINT('',#129945);
#12100=VERTEX_POINT('',#130186);
#12101=VERTEX_POINT('',#130187);
#12102=VERTEX_POINT('',#130189);
#12103=VERTEX_POINT('',#130426);
#12104=VERTEX_POINT('',#130482);
#12105=VERTEX_POINT('',#130483);
#12106=VERTEX_POINT('',#130485);
#12107=VERTEX_POINT('',#130494);
#12108=VERTEX_POINT('',#130553);
#12109=VERTEX_POINT('',#130555);
#12110=VERTEX_POINT('',#130570);
#12111=VERTEX_POINT('',#130571);
#12112=VERTEX_POINT('',#130573);
#12113=VERTEX_POINT('',#130589);
#12114=VERTEX_POINT('',#130721);
#12115=VERTEX_POINT('',#130722);
#12116=VERTEX_POINT('',#130724);
#12117=VERTEX_POINT('',#130855);
#12118=VERTEX_POINT('',#131054);
#12119=VERTEX_POINT('',#131055);
#12120=VERTEX_POINT('',#131057);
#12121=VERTEX_POINT('',#131255);
#12122=VERTEX_POINT('',#131335);
#12123=VERTEX_POINT('',#131336);
#12124=VERTEX_POINT('',#131338);
#12125=VERTEX_POINT('',#131536);
#12126=VERTEX_POINT('',#131671);
#12127=VERTEX_POINT('',#131672);
#12128=VERTEX_POINT('',#131674);
#12129=VERTEX_POINT('',#131753);
#12130=VERTEX_POINT('',#131833);
#12131=VERTEX_POINT('',#131834);
#12132=VERTEX_POINT('',#131836);
#12133=VERTEX_POINT('',#131967);
#12134=VERTEX_POINT('',#132103);
#12135=VERTEX_POINT('',#132104);
#12136=VERTEX_POINT('',#132106);
#12137=VERTEX_POINT('',#132185);
#12138=VERTEX_POINT('',#132378);
#12139=VERTEX_POINT('',#132379);
#12140=VERTEX_POINT('',#132381);
#12141=VERTEX_POINT('',#132516);
#12142=VERTEX_POINT('',#132712);
#12143=VERTEX_POINT('',#132713);
#12144=VERTEX_POINT('',#132715);
#12145=VERTEX_POINT('',#132794);
#12146=VERTEX_POINT('',#132874);
#12147=VERTEX_POINT('',#132875);
#12148=VERTEX_POINT('',#132877);
#12149=VERTEX_POINT('',#133008);
#12150=VERTEX_POINT('',#133141);
#12151=VERTEX_POINT('',#133142);
#12152=VERTEX_POINT('',#133144);
#12153=VERTEX_POINT('',#133223);
#12154=VERTEX_POINT('',#133419);
#12155=VERTEX_POINT('',#133420);
#12156=VERTEX_POINT('',#133422);
#12157=VERTEX_POINT('',#133553);
#12158=VERTEX_POINT('',#133752);
#12159=VERTEX_POINT('',#133753);
#12160=VERTEX_POINT('',#133755);
#12161=VERTEX_POINT('',#133837);
#12162=VERTEX_POINT('',#133917);
#12163=VERTEX_POINT('',#133918);
#12164=VERTEX_POINT('',#133920);
#12165=VERTEX_POINT('',#134051);
#12166=VERTEX_POINT('',#134186);
#12167=VERTEX_POINT('',#134187);
#12168=VERTEX_POINT('',#134189);
#12169=VERTEX_POINT('',#134387);
#12170=VERTEX_POINT('',#134467);
#12171=VERTEX_POINT('',#134468);
#12172=VERTEX_POINT('',#134470);
#12173=VERTEX_POINT('',#134665);
#12174=VERTEX_POINT('',#134800);
#12175=VERTEX_POINT('',#134801);
#12176=VERTEX_POINT('',#134803);
#12177=VERTEX_POINT('',#134882);
#12178=VERTEX_POINT('',#134959);
#12179=VERTEX_POINT('',#134960);
#12180=VERTEX_POINT('',#134962);
#12181=VERTEX_POINT('',#135097);
#12182=VERTEX_POINT('',#135229);
#12183=VERTEX_POINT('',#135230);
#12184=VERTEX_POINT('',#135232);
#12185=VERTEX_POINT('',#135430);
#12186=VERTEX_POINT('',#135510);
#12187=VERTEX_POINT('',#135511);
#12188=VERTEX_POINT('',#135513);
#12189=VERTEX_POINT('',#135708);
#12190=VERTEX_POINT('',#135841);
#12191=VERTEX_POINT('',#135842);
#12192=VERTEX_POINT('',#135844);
#12193=VERTEX_POINT('',#135924);
#12194=VERTEX_POINT('',#136004);
#12195=VERTEX_POINT('',#136005);
#12196=VERTEX_POINT('',#136007);
#12197=VERTEX_POINT('',#136138);
#12198=VERTEX_POINT('',#136270);
#12199=VERTEX_POINT('',#136271);
#12200=VERTEX_POINT('',#136273);
#12201=VERTEX_POINT('',#136352);
#12202=VERTEX_POINT('',#136551);
#12203=VERTEX_POINT('',#136552);
#12204=VERTEX_POINT('',#136554);
#12205=VERTEX_POINT('',#136685);
#12206=VERTEX_POINT('',#136884);
#12207=VERTEX_POINT('',#136885);
#12208=VERTEX_POINT('',#136887);
#12209=VERTEX_POINT('',#137085);
#12210=VERTEX_POINT('',#137165);
#12211=VERTEX_POINT('',#137166);
#12212=VERTEX_POINT('',#137168);
#12213=VERTEX_POINT('',#137247);
#12214=VERTEX_POINT('',#137263);
#12215=VERTEX_POINT('',#137264);
#12216=VERTEX_POINT('',#137266);
#12217=VERTEX_POINT('',#137275);
#12218=VERTEX_POINT('',#137334);
#12219=VERTEX_POINT('',#137336);
#12220=VERTEX_POINT('',#137351);
#12221=VERTEX_POINT('',#137352);
#12222=VERTEX_POINT('',#137354);
#12223=VERTEX_POINT('',#137370);
#12224=VERTEX_POINT('',#137502);
#12225=VERTEX_POINT('',#137503);
#12226=VERTEX_POINT('',#137505);
#12227=VERTEX_POINT('',#137636);
#12228=VERTEX_POINT('',#137835);
#12229=VERTEX_POINT('',#137836);
#12230=VERTEX_POINT('',#137838);
#12231=VERTEX_POINT('',#138036);
#12232=VERTEX_POINT('',#138116);
#12233=VERTEX_POINT('',#138117);
#12234=VERTEX_POINT('',#138119);
#12235=VERTEX_POINT('',#138317);
#12236=VERTEX_POINT('',#138452);
#12237=VERTEX_POINT('',#138453);
#12238=VERTEX_POINT('',#138455);
#12239=VERTEX_POINT('',#138534);
#12240=VERTEX_POINT('',#138614);
#12241=VERTEX_POINT('',#138615);
#12242=VERTEX_POINT('',#138617);
#12243=VERTEX_POINT('',#138748);
#12244=VERTEX_POINT('',#138884);
#12245=VERTEX_POINT('',#138885);
#12246=VERTEX_POINT('',#138887);
#12247=VERTEX_POINT('',#138966);
#12248=VERTEX_POINT('',#139159);
#12249=VERTEX_POINT('',#139160);
#12250=VERTEX_POINT('',#139162);
#12251=VERTEX_POINT('',#139297);
#12252=VERTEX_POINT('',#139493);
#12253=VERTEX_POINT('',#139494);
#12254=VERTEX_POINT('',#139496);
#12255=VERTEX_POINT('',#139575);
#12256=VERTEX_POINT('',#139655);
#12257=VERTEX_POINT('',#139656);
#12258=VERTEX_POINT('',#139658);
#12259=VERTEX_POINT('',#139789);
#12260=VERTEX_POINT('',#139922);
#12261=VERTEX_POINT('',#139923);
#12262=VERTEX_POINT('',#139925);
#12263=VERTEX_POINT('',#140004);
#12264=VERTEX_POINT('',#140200);
#12265=VERTEX_POINT('',#140201);
#12266=VERTEX_POINT('',#140203);
#12267=VERTEX_POINT('',#140334);
#12268=VERTEX_POINT('',#140533);
#12269=VERTEX_POINT('',#140534);
#12270=VERTEX_POINT('',#140536);
#12271=VERTEX_POINT('',#140618);
#12272=VERTEX_POINT('',#140698);
#12273=VERTEX_POINT('',#140699);
#12274=VERTEX_POINT('',#140701);
#12275=VERTEX_POINT('',#140832);
#12276=VERTEX_POINT('',#140967);
#12277=VERTEX_POINT('',#140968);
#12278=VERTEX_POINT('',#140970);
#12279=VERTEX_POINT('',#141168);
#12280=VERTEX_POINT('',#141248);
#12281=VERTEX_POINT('',#141249);
#12282=VERTEX_POINT('',#141251);
#12283=VERTEX_POINT('',#141446);
#12284=VERTEX_POINT('',#141581);
#12285=VERTEX_POINT('',#141582);
#12286=VERTEX_POINT('',#141584);
#12287=VERTEX_POINT('',#141663);
#12288=VERTEX_POINT('',#141740);
#12289=VERTEX_POINT('',#141741);
#12290=VERTEX_POINT('',#141743);
#12291=VERTEX_POINT('',#141878);
#12292=VERTEX_POINT('',#142010);
#12293=VERTEX_POINT('',#142011);
#12294=VERTEX_POINT('',#142013);
#12295=VERTEX_POINT('',#142211);
#12296=VERTEX_POINT('',#142291);
#12297=VERTEX_POINT('',#142292);
#12298=VERTEX_POINT('',#142294);
#12299=VERTEX_POINT('',#142489);
#12300=VERTEX_POINT('',#142622);
#12301=VERTEX_POINT('',#142623);
#12302=VERTEX_POINT('',#142625);
#12303=VERTEX_POINT('',#142705);
#12304=VERTEX_POINT('',#142785);
#12305=VERTEX_POINT('',#142786);
#12306=VERTEX_POINT('',#142788);
#12307=VERTEX_POINT('',#142919);
#12308=VERTEX_POINT('',#143051);
#12309=VERTEX_POINT('',#143052);
#12310=VERTEX_POINT('',#143054);
#12311=VERTEX_POINT('',#143133);
#12312=VERTEX_POINT('',#143332);
#12313=VERTEX_POINT('',#143333);
#12314=VERTEX_POINT('',#143335);
#12315=VERTEX_POINT('',#143466);
#12316=VERTEX_POINT('',#143665);
#12317=VERTEX_POINT('',#143666);
#12318=VERTEX_POINT('',#143668);
#12319=VERTEX_POINT('',#143866);
#12320=VERTEX_POINT('',#143946);
#12321=VERTEX_POINT('',#143947);
#12322=VERTEX_POINT('',#143949);
#12323=VERTEX_POINT('',#144028);
#12324=VERTEX_POINT('',#144044);
#12325=VERTEX_POINT('',#144045);
#12326=VERTEX_POINT('',#144047);
#12327=VERTEX_POINT('',#144056);
#12328=VERTEX_POINT('',#144115);
#12329=VERTEX_POINT('',#144117);
#12330=VERTEX_POINT('',#144132);
#12331=VERTEX_POINT('',#144133);
#12332=VERTEX_POINT('',#144135);
#12333=VERTEX_POINT('',#144151);
#12334=VERTEX_POINT('',#144283);
#12335=VERTEX_POINT('',#144284);
#12336=VERTEX_POINT('',#144286);
#12337=VERTEX_POINT('',#144417);
#12338=VERTEX_POINT('',#144616);
#12339=VERTEX_POINT('',#144617);
#12340=VERTEX_POINT('',#144619);
#12341=VERTEX_POINT('',#144817);
#12342=VERTEX_POINT('',#144897);
#12343=VERTEX_POINT('',#144898);
#12344=VERTEX_POINT('',#144900);
#12345=VERTEX_POINT('',#145098);
#12346=VERTEX_POINT('',#145233);
#12347=VERTEX_POINT('',#145234);
#12348=VERTEX_POINT('',#145236);
#12349=VERTEX_POINT('',#145315);
#12350=VERTEX_POINT('',#145395);
#12351=VERTEX_POINT('',#145396);
#12352=VERTEX_POINT('',#145398);
#12353=VERTEX_POINT('',#145529);
#12354=VERTEX_POINT('',#145665);
#12355=VERTEX_POINT('',#145666);
#12356=VERTEX_POINT('',#145668);
#12357=VERTEX_POINT('',#145747);
#12358=VERTEX_POINT('',#145940);
#12359=VERTEX_POINT('',#145941);
#12360=VERTEX_POINT('',#145943);
#12361=VERTEX_POINT('',#146078);
#12362=VERTEX_POINT('',#146274);
#12363=VERTEX_POINT('',#146275);
#12364=VERTEX_POINT('',#146277);
#12365=VERTEX_POINT('',#146356);
#12366=VERTEX_POINT('',#146436);
#12367=VERTEX_POINT('',#146437);
#12368=VERTEX_POINT('',#146439);
#12369=VERTEX_POINT('',#146570);
#12370=VERTEX_POINT('',#146703);
#12371=VERTEX_POINT('',#146704);
#12372=VERTEX_POINT('',#146706);
#12373=VERTEX_POINT('',#146785);
#12374=VERTEX_POINT('',#146981);
#12375=VERTEX_POINT('',#146982);
#12376=VERTEX_POINT('',#146984);
#12377=VERTEX_POINT('',#147115);
#12378=VERTEX_POINT('',#147314);
#12379=VERTEX_POINT('',#147315);
#12380=VERTEX_POINT('',#147317);
#12381=VERTEX_POINT('',#147399);
#12382=VERTEX_POINT('',#147479);
#12383=VERTEX_POINT('',#147480);
#12384=VERTEX_POINT('',#147482);
#12385=VERTEX_POINT('',#147613);
#12386=VERTEX_POINT('',#147748);
#12387=VERTEX_POINT('',#147749);
#12388=VERTEX_POINT('',#147751);
#12389=VERTEX_POINT('',#147949);
#12390=VERTEX_POINT('',#148029);
#12391=VERTEX_POINT('',#148030);
#12392=VERTEX_POINT('',#148032);
#12393=VERTEX_POINT('',#148227);
#12394=VERTEX_POINT('',#148362);
#12395=VERTEX_POINT('',#148363);
#12396=VERTEX_POINT('',#148365);
#12397=VERTEX_POINT('',#148444);
#12398=VERTEX_POINT('',#148521);
#12399=VERTEX_POINT('',#148522);
#12400=VERTEX_POINT('',#148524);
#12401=VERTEX_POINT('',#148659);
#12402=VERTEX_POINT('',#148791);
#12403=VERTEX_POINT('',#148792);
#12404=VERTEX_POINT('',#148794);
#12405=VERTEX_POINT('',#148992);
#12406=VERTEX_POINT('',#149072);
#12407=VERTEX_POINT('',#149073);
#12408=VERTEX_POINT('',#149075);
#12409=VERTEX_POINT('',#149270);
#12410=VERTEX_POINT('',#149403);
#12411=VERTEX_POINT('',#149404);
#12412=VERTEX_POINT('',#149406);
#12413=VERTEX_POINT('',#149486);
#12414=VERTEX_POINT('',#149566);
#12415=VERTEX_POINT('',#149567);
#12416=VERTEX_POINT('',#149569);
#12417=VERTEX_POINT('',#149700);
#12418=VERTEX_POINT('',#149832);
#12419=VERTEX_POINT('',#149833);
#12420=VERTEX_POINT('',#149835);
#12421=VERTEX_POINT('',#149914);
#12422=VERTEX_POINT('',#150113);
#12423=VERTEX_POINT('',#150114);
#12424=VERTEX_POINT('',#150116);
#12425=VERTEX_POINT('',#150247);
#12426=VERTEX_POINT('',#150446);
#12427=VERTEX_POINT('',#150447);
#12428=VERTEX_POINT('',#150449);
#12429=VERTEX_POINT('',#150647);
#12430=VERTEX_POINT('',#150727);
#12431=VERTEX_POINT('',#150728);
#12432=VERTEX_POINT('',#150730);
#12433=VERTEX_POINT('',#150809);
#12434=VERTEX_POINT('',#150825);
#12435=VERTEX_POINT('',#150826);
#12436=VERTEX_POINT('',#150828);
#12437=VERTEX_POINT('',#150837);
#12438=VERTEX_POINT('',#150896);
#12439=VERTEX_POINT('',#150898);
#12440=VERTEX_POINT('',#150913);
#12441=VERTEX_POINT('',#150914);
#12442=VERTEX_POINT('',#150916);
#12443=VERTEX_POINT('',#150932);
#12444=VERTEX_POINT('',#151064);
#12445=VERTEX_POINT('',#151065);
#12446=VERTEX_POINT('',#151067);
#12447=VERTEX_POINT('',#151198);
#12448=VERTEX_POINT('',#151397);
#12449=VERTEX_POINT('',#151398);
#12450=VERTEX_POINT('',#151400);
#12451=VERTEX_POINT('',#151598);
#12452=VERTEX_POINT('',#151678);
#12453=VERTEX_POINT('',#151679);
#12454=VERTEX_POINT('',#151681);
#12455=VERTEX_POINT('',#151879);
#12456=VERTEX_POINT('',#152014);
#12457=VERTEX_POINT('',#152015);
#12458=VERTEX_POINT('',#152017);
#12459=VERTEX_POINT('',#152096);
#12460=VERTEX_POINT('',#152176);
#12461=VERTEX_POINT('',#152177);
#12462=VERTEX_POINT('',#152179);
#12463=VERTEX_POINT('',#152310);
#12464=VERTEX_POINT('',#152446);
#12465=VERTEX_POINT('',#152447);
#12466=VERTEX_POINT('',#152449);
#12467=VERTEX_POINT('',#152528);
#12468=VERTEX_POINT('',#152721);
#12469=VERTEX_POINT('',#152722);
#12470=VERTEX_POINT('',#152724);
#12471=VERTEX_POINT('',#152859);
#12472=VERTEX_POINT('',#153055);
#12473=VERTEX_POINT('',#153056);
#12474=VERTEX_POINT('',#153058);
#12475=VERTEX_POINT('',#153137);
#12476=VERTEX_POINT('',#153217);
#12477=VERTEX_POINT('',#153218);
#12478=VERTEX_POINT('',#153220);
#12479=VERTEX_POINT('',#153351);
#12480=VERTEX_POINT('',#153484);
#12481=VERTEX_POINT('',#153485);
#12482=VERTEX_POINT('',#153487);
#12483=VERTEX_POINT('',#153566);
#12484=VERTEX_POINT('',#153762);
#12485=VERTEX_POINT('',#153763);
#12486=VERTEX_POINT('',#153765);
#12487=VERTEX_POINT('',#153896);
#12488=VERTEX_POINT('',#154095);
#12489=VERTEX_POINT('',#154096);
#12490=VERTEX_POINT('',#154098);
#12491=VERTEX_POINT('',#154180);
#12492=VERTEX_POINT('',#154260);
#12493=VERTEX_POINT('',#154261);
#12494=VERTEX_POINT('',#154263);
#12495=VERTEX_POINT('',#154394);
#12496=VERTEX_POINT('',#154529);
#12497=VERTEX_POINT('',#154530);
#12498=VERTEX_POINT('',#154532);
#12499=VERTEX_POINT('',#154730);
#12500=VERTEX_POINT('',#154810);
#12501=VERTEX_POINT('',#154811);
#12502=VERTEX_POINT('',#154813);
#12503=VERTEX_POINT('',#155008);
#12504=VERTEX_POINT('',#155143);
#12505=VERTEX_POINT('',#155144);
#12506=VERTEX_POINT('',#155146);
#12507=VERTEX_POINT('',#155225);
#12508=VERTEX_POINT('',#155302);
#12509=VERTEX_POINT('',#155303);
#12510=VERTEX_POINT('',#155305);
#12511=VERTEX_POINT('',#155440);
#12512=VERTEX_POINT('',#155572);
#12513=VERTEX_POINT('',#155573);
#12514=VERTEX_POINT('',#155575);
#12515=VERTEX_POINT('',#155773);
#12516=VERTEX_POINT('',#155853);
#12517=VERTEX_POINT('',#155854);
#12518=VERTEX_POINT('',#155856);
#12519=VERTEX_POINT('',#156051);
#12520=VERTEX_POINT('',#156184);
#12521=VERTEX_POINT('',#156185);
#12522=VERTEX_POINT('',#156187);
#12523=VERTEX_POINT('',#156267);
#12524=VERTEX_POINT('',#156347);
#12525=VERTEX_POINT('',#156348);
#12526=VERTEX_POINT('',#156350);
#12527=VERTEX_POINT('',#156481);
#12528=VERTEX_POINT('',#156613);
#12529=VERTEX_POINT('',#156614);
#12530=VERTEX_POINT('',#156616);
#12531=VERTEX_POINT('',#156695);
#12532=VERTEX_POINT('',#156894);
#12533=VERTEX_POINT('',#156895);
#12534=VERTEX_POINT('',#156897);
#12535=VERTEX_POINT('',#157028);
#12536=VERTEX_POINT('',#157227);
#12537=VERTEX_POINT('',#157228);
#12538=VERTEX_POINT('',#157230);
#12539=VERTEX_POINT('',#157428);
#12540=VERTEX_POINT('',#157508);
#12541=VERTEX_POINT('',#157509);
#12542=VERTEX_POINT('',#157511);
#12543=VERTEX_POINT('',#157590);
#12544=VERTEX_POINT('',#157606);
#12545=VERTEX_POINT('',#157607);
#12546=VERTEX_POINT('',#157609);
#12547=VERTEX_POINT('',#157628);
#12548=VERTEX_POINT('',#157629);
#12549=VERTEX_POINT('',#157685);
#12550=VERTEX_POINT('',#157740);
#12551=VERTEX_POINT('',#157741);
#12552=VERTEX_POINT('',#158028);
#12553=VERTEX_POINT('',#158029);
#12554=VERTEX_POINT('',#158314);
#12555=VERTEX_POINT('',#158315);
#12556=VERTEX_POINT('',#158317);
#12557=VERTEX_POINT('',#158333);
#12558=VERTEX_POINT('',#158370);
#12559=VERTEX_POINT('',#158371);
#12560=VERTEX_POINT('',#158656);
#12561=VERTEX_POINT('',#158657);
#12562=VERTEX_POINT('',#158946);
#12563=VERTEX_POINT('',#158947);
#12564=VERTEX_POINT('',#158949);
#12565=VERTEX_POINT('',#159058);
#12566=VERTEX_POINT('',#159059);
#12567=VERTEX_POINT('',#159061);
#12568=VERTEX_POINT('',#159072);
#12569=VERTEX_POINT('',#159242);
#12570=VERTEX_POINT('',#159244);
#12571=VERTEX_POINT('',#159390);
#12572=VERTEX_POINT('',#159391);
#12573=VERTEX_POINT('',#159393);
#12574=VERTEX_POINT('',#159826);
#12575=VERTEX_POINT('',#159827);
#12576=VERTEX_POINT('',#160069);
#12577=VERTEX_POINT('',#160285);
#12578=VERTEX_POINT('',#160286);
#12579=VERTEX_POINT('',#160288);
#12580=VERTEX_POINT('',#160557);
#12581=VERTEX_POINT('',#160587);
#12582=VERTEX_POINT('',#160588);
#12583=VERTEX_POINT('',#161059);
#12584=VERTEX_POINT('',#161060);
#12585=VERTEX_POINT('',#161062);
#12586=VERTEX_POINT('',#161301);
#12587=VERTEX_POINT('',#161549);
#12588=VERTEX_POINT('',#161550);
#12589=VERTEX_POINT('',#162067);
#12590=VERTEX_POINT('',#162068);
#12591=VERTEX_POINT('',#162070);
#12592=VERTEX_POINT('',#162305);
#12593=VERTEX_POINT('',#162546);
#12594=VERTEX_POINT('',#162547);
#12595=VERTEX_POINT('',#162781);
#12596=VERTEX_POINT('',#162965);
#12597=VERTEX_POINT('',#162966);
#12598=VERTEX_POINT('',#162968);
#12599=VERTEX_POINT('',#163203);
#12600=VERTEX_POINT('',#163233);
#12601=VERTEX_POINT('',#163234);
#12602=VERTEX_POINT('',#163691);
#12603=VERTEX_POINT('',#163692);
#12604=VERTEX_POINT('',#163694);
#12605=VERTEX_POINT('',#163920);
#12606=VERTEX_POINT('',#164154);
#12607=VERTEX_POINT('',#164155);
#12608=VERTEX_POINT('',#164157);
#12609=VERTEX_POINT('',#164454);
#12610=VERTEX_POINT('',#164455);
#12611=VERTEX_POINT('',#164457);
#12612=VERTEX_POINT('',#164665);
#12613=VERTEX_POINT('',#164895);
#12614=VERTEX_POINT('',#164896);
#12615=VERTEX_POINT('',#165130);
#12616=VERTEX_POINT('',#165318);
#12617=VERTEX_POINT('',#165319);
#12618=VERTEX_POINT('',#165321);
#12619=VERTEX_POINT('',#165584);
#12620=VERTEX_POINT('',#165616);
#12621=VERTEX_POINT('',#165617);
#12622=VERTEX_POINT('',#166080);
#12623=VERTEX_POINT('',#166081);
#12624=VERTEX_POINT('',#166083);
#12625=VERTEX_POINT('',#166306);
#12626=VERTEX_POINT('',#166548);
#12627=VERTEX_POINT('',#166549);
#12628=VERTEX_POINT('',#166551);
#12629=VERTEX_POINT('',#166791);
#12630=VERTEX_POINT('',#166792);
#12631=VERTEX_POINT('',#166794);
#12632=VERTEX_POINT('',#166981);
#12633=VERTEX_POINT('',#167223);
#12634=VERTEX_POINT('',#167224);
#12635=VERTEX_POINT('',#167691);
#12636=VERTEX_POINT('',#167692);
#12637=VERTEX_POINT('',#167694);
#12638=VERTEX_POINT('',#167945);
#12639=VERTEX_POINT('',#168201);
#12640=VERTEX_POINT('',#168202);
#12641=VERTEX_POINT('',#168671);
#12642=VERTEX_POINT('',#168672);
#12643=VERTEX_POINT('',#168674);
#12644=VERTEX_POINT('',#168905);
#12645=VERTEX_POINT('',#169137);
#12646=VERTEX_POINT('',#169138);
#12647=VERTEX_POINT('',#169140);
#12648=VERTEX_POINT('',#169436);
#12649=VERTEX_POINT('',#169437);
#12650=VERTEX_POINT('',#169673);
#12651=VERTEX_POINT('',#169914);
#12652=VERTEX_POINT('',#169915);
#12653=VERTEX_POINT('',#169917);
#12654=VERTEX_POINT('',#170153);
#12655=VERTEX_POINT('',#170349);
#12656=VERTEX_POINT('',#170350);
#12657=VERTEX_POINT('',#170352);
#12658=VERTEX_POINT('',#170363);
#12659=VERTEX_POINT('',#170533);
#12660=VERTEX_POINT('',#170535);
#12661=VERTEX_POINT('',#170681);
#12662=VERTEX_POINT('',#170682);
#12663=VERTEX_POINT('',#170684);
#12664=VERTEX_POINT('',#171117);
#12665=VERTEX_POINT('',#171118);
#12666=VERTEX_POINT('',#171356);
#12667=VERTEX_POINT('',#171572);
#12668=VERTEX_POINT('',#171573);
#12669=VERTEX_POINT('',#171575);
#12670=VERTEX_POINT('',#171846);
#12671=VERTEX_POINT('',#171876);
#12672=VERTEX_POINT('',#171877);
#12673=VERTEX_POINT('',#172348);
#12674=VERTEX_POINT('',#172349);
#12675=VERTEX_POINT('',#172351);
#12676=VERTEX_POINT('',#172580);
#12677=VERTEX_POINT('',#172830);
#12678=VERTEX_POINT('',#172831);
#12679=VERTEX_POINT('',#173336);
#12680=VERTEX_POINT('',#173337);
#12681=VERTEX_POINT('',#173339);
#12682=VERTEX_POINT('',#173580);
#12683=VERTEX_POINT('',#173817);
#12684=VERTEX_POINT('',#173818);
#12685=VERTEX_POINT('',#174098);
#12686=VERTEX_POINT('',#174282);
#12687=VERTEX_POINT('',#174283);
#12688=VERTEX_POINT('',#174285);
#12689=VERTEX_POINT('',#174520);
#12690=VERTEX_POINT('',#174550);
#12691=VERTEX_POINT('',#174551);
#12692=VERTEX_POINT('',#175008);
#12693=VERTEX_POINT('',#175009);
#12694=VERTEX_POINT('',#175011);
#12695=VERTEX_POINT('',#175239);
#12696=VERTEX_POINT('',#175471);
#12697=VERTEX_POINT('',#175472);
#12698=VERTEX_POINT('',#175474);
#12699=VERTEX_POINT('',#175771);
#12700=VERTEX_POINT('',#175772);
#12701=VERTEX_POINT('',#175774);
#12702=VERTEX_POINT('',#175982);
#12703=VERTEX_POINT('',#176222);
#12704=VERTEX_POINT('',#176223);
#12705=VERTEX_POINT('',#176459);
#12706=VERTEX_POINT('',#176647);
#12707=VERTEX_POINT('',#176648);
#12708=VERTEX_POINT('',#176650);
#12709=VERTEX_POINT('',#176901);
#12710=VERTEX_POINT('',#176933);
#12711=VERTEX_POINT('',#176934);
#12712=VERTEX_POINT('',#177401);
#12713=VERTEX_POINT('',#177402);
#12714=VERTEX_POINT('',#177404);
#12715=VERTEX_POINT('',#177625);
#12716=VERTEX_POINT('',#177869);
#12717=VERTEX_POINT('',#177870);
#12718=VERTEX_POINT('',#177872);
#12719=VERTEX_POINT('',#178112);
#12720=VERTEX_POINT('',#178113);
#12721=VERTEX_POINT('',#178115);
#12722=VERTEX_POINT('',#178302);
#12723=VERTEX_POINT('',#178544);
#12724=VERTEX_POINT('',#178545);
#12725=VERTEX_POINT('',#179014);
#12726=VERTEX_POINT('',#179015);
#12727=VERTEX_POINT('',#179017);
#12728=VERTEX_POINT('',#179264);
#12729=VERTEX_POINT('',#179544);
#12730=VERTEX_POINT('',#179545);
#12731=VERTEX_POINT('',#180014);
#12732=VERTEX_POINT('',#180015);
#12733=VERTEX_POINT('',#180017);
#12734=VERTEX_POINT('',#180248);
#12735=VERTEX_POINT('',#180478);
#12736=VERTEX_POINT('',#180479);
#12737=VERTEX_POINT('',#180481);
#12738=VERTEX_POINT('',#180747);
#12739=VERTEX_POINT('',#180748);
#12740=VERTEX_POINT('',#180984);
#12741=VERTEX_POINT('',#181225);
#12742=VERTEX_POINT('',#181226);
#12743=VERTEX_POINT('',#181228);
#12744=VERTEX_POINT('',#181464);
#12745=VERTEX_POINT('',#181660);
#12746=VERTEX_POINT('',#181661);
#12747=VERTEX_POINT('',#181663);
#12748=VERTEX_POINT('',#181674);
#12749=VERTEX_POINT('',#181844);
#12750=VERTEX_POINT('',#181846);
#12751=VERTEX_POINT('',#181992);
#12752=VERTEX_POINT('',#181993);
#12753=VERTEX_POINT('',#181995);
#12754=VERTEX_POINT('',#182428);
#12755=VERTEX_POINT('',#182429);
#12756=VERTEX_POINT('',#182671);
#12757=VERTEX_POINT('',#182887);
#12758=VERTEX_POINT('',#182888);
#12759=VERTEX_POINT('',#182890);
#12760=VERTEX_POINT('',#183157);
#12761=VERTEX_POINT('',#183189);
#12762=VERTEX_POINT('',#183190);
#12763=VERTEX_POINT('',#183649);
#12764=VERTEX_POINT('',#183650);
#12765=VERTEX_POINT('',#183652);
#12766=VERTEX_POINT('',#183881);
#12767=VERTEX_POINT('',#184131);
#12768=VERTEX_POINT('',#184132);
#12769=VERTEX_POINT('',#184641);
#12770=VERTEX_POINT('',#184642);
#12771=VERTEX_POINT('',#184644);
#12772=VERTEX_POINT('',#184877);
#12773=VERTEX_POINT('',#185112);
#12774=VERTEX_POINT('',#185113);
#12775=VERTEX_POINT('',#185351);
#12776=VERTEX_POINT('',#185535);
#12777=VERTEX_POINT('',#185536);
#12778=VERTEX_POINT('',#185538);
#12779=VERTEX_POINT('',#185773);
#12780=VERTEX_POINT('',#185803);
#12781=VERTEX_POINT('',#185804);
#12782=VERTEX_POINT('',#186263);
#12783=VERTEX_POINT('',#186264);
#12784=VERTEX_POINT('',#186266);
#12785=VERTEX_POINT('',#186494);
#12786=VERTEX_POINT('',#186726);
#12787=VERTEX_POINT('',#186727);
#12788=VERTEX_POINT('',#186729);
#12789=VERTEX_POINT('',#187050);
#12790=VERTEX_POINT('',#187051);
#12791=VERTEX_POINT('',#187053);
#12792=VERTEX_POINT('',#187261);
#12793=VERTEX_POINT('',#187535);
#12794=VERTEX_POINT('',#187536);
#12795=VERTEX_POINT('',#187808);
#12796=VERTEX_POINT('',#187996);
#12797=VERTEX_POINT('',#187997);
#12798=VERTEX_POINT('',#187999);
#12799=VERTEX_POINT('',#188264);
#12800=VERTEX_POINT('',#188296);
#12801=VERTEX_POINT('',#188297);
#12802=VERTEX_POINT('',#188760);
#12803=VERTEX_POINT('',#188761);
#12804=VERTEX_POINT('',#188763);
#12805=VERTEX_POINT('',#188984);
#12806=VERTEX_POINT('',#189228);
#12807=VERTEX_POINT('',#189229);
#12808=VERTEX_POINT('',#189231);
#12809=VERTEX_POINT('',#189471);
#12810=VERTEX_POINT('',#189472);
#12811=VERTEX_POINT('',#189474);
#12812=VERTEX_POINT('',#189661);
#12813=VERTEX_POINT('',#189903);
#12814=VERTEX_POINT('',#189904);
#12815=VERTEX_POINT('',#190379);
#12816=VERTEX_POINT('',#190380);
#12817=VERTEX_POINT('',#190382);
#12818=VERTEX_POINT('',#190633);
#12819=VERTEX_POINT('',#190889);
#12820=VERTEX_POINT('',#190890);
#12821=VERTEX_POINT('',#191363);
#12822=VERTEX_POINT('',#191364);
#12823=VERTEX_POINT('',#191366);
#12824=VERTEX_POINT('',#191589);
#12825=VERTEX_POINT('',#191821);
#12826=VERTEX_POINT('',#191822);
#12827=VERTEX_POINT('',#191824);
#12828=VERTEX_POINT('',#192076);
#12829=VERTEX_POINT('',#192077);
#12830=VERTEX_POINT('',#192313);
#12831=VERTEX_POINT('',#192556);
#12832=VERTEX_POINT('',#192557);
#12833=VERTEX_POINT('',#192559);
#12834=VERTEX_POINT('',#192795);
#12835=VERTEX_POINT('',#192991);
#12836=VERTEX_POINT('',#192992);
#12837=VERTEX_POINT('',#192994);
#12838=VERTEX_POINT('',#193005);
#12839=VERTEX_POINT('',#193175);
#12840=VERTEX_POINT('',#193177);
#12841=VERTEX_POINT('',#193323);
#12842=VERTEX_POINT('',#193324);
#12843=VERTEX_POINT('',#193326);
#12844=VERTEX_POINT('',#193759);
#12845=VERTEX_POINT('',#193760);
#12846=VERTEX_POINT('',#194000);
#12847=VERTEX_POINT('',#194216);
#12848=VERTEX_POINT('',#194217);
#12849=VERTEX_POINT('',#194219);
#12850=VERTEX_POINT('',#194488);
#12851=VERTEX_POINT('',#194520);
#12852=VERTEX_POINT('',#194521);
#12853=VERTEX_POINT('',#194982);
#12854=VERTEX_POINT('',#194983);
#12855=VERTEX_POINT('',#194985);
#12856=VERTEX_POINT('',#195214);
#12857=VERTEX_POINT('',#195460);
#12858=VERTEX_POINT('',#195461);
#12859=VERTEX_POINT('',#195952);
#12860=VERTEX_POINT('',#195953);
#12861=VERTEX_POINT('',#195955);
#12862=VERTEX_POINT('',#196190);
#12863=VERTEX_POINT('',#196423);
#12864=VERTEX_POINT('',#196424);
#12865=VERTEX_POINT('',#196708);
#12866=VERTEX_POINT('',#196892);
#12867=VERTEX_POINT('',#196893);
#12868=VERTEX_POINT('',#196895);
#12869=VERTEX_POINT('',#197130);
#12870=VERTEX_POINT('',#197160);
#12871=VERTEX_POINT('',#197161);
#12872=VERTEX_POINT('',#197626);
#12873=VERTEX_POINT('',#197627);
#12874=VERTEX_POINT('',#197629);
#12875=VERTEX_POINT('',#197857);
#12876=VERTEX_POINT('',#198091);
#12877=VERTEX_POINT('',#198092);
#12878=VERTEX_POINT('',#198094);
#12879=VERTEX_POINT('',#198389);
#12880=VERTEX_POINT('',#198390);
#12881=VERTEX_POINT('',#198392);
#12882=VERTEX_POINT('',#198600);
#12883=VERTEX_POINT('',#198840);
#12884=VERTEX_POINT('',#198841);
#12885=VERTEX_POINT('',#199077);
#12886=VERTEX_POINT('',#199265);
#12887=VERTEX_POINT('',#199266);
#12888=VERTEX_POINT('',#199268);
#12889=VERTEX_POINT('',#199527);
#12890=VERTEX_POINT('',#199559);
#12891=VERTEX_POINT('',#199560);
#12892=VERTEX_POINT('',#200025);
#12893=VERTEX_POINT('',#200026);
#12894=VERTEX_POINT('',#200028);
#12895=VERTEX_POINT('',#200253);
#12896=VERTEX_POINT('',#200493);
#12897=VERTEX_POINT('',#200494);
#12898=VERTEX_POINT('',#200496);
#12899=VERTEX_POINT('',#200736);
#12900=VERTEX_POINT('',#200737);
#12901=VERTEX_POINT('',#200739);
#12902=VERTEX_POINT('',#200926);
#12903=VERTEX_POINT('',#201214);
#12904=VERTEX_POINT('',#201215);
#12905=VERTEX_POINT('',#201692);
#12906=VERTEX_POINT('',#201693);
#12907=VERTEX_POINT('',#201695);
#12908=VERTEX_POINT('',#201944);
#12909=VERTEX_POINT('',#202220);
#12910=VERTEX_POINT('',#202221);
#12911=VERTEX_POINT('',#202694);
#12912=VERTEX_POINT('',#202695);
#12913=VERTEX_POINT('',#202697);
#12914=VERTEX_POINT('',#202912);
#12915=VERTEX_POINT('',#203140);
#12916=VERTEX_POINT('',#203141);
#12917=VERTEX_POINT('',#203143);
#12918=VERTEX_POINT('',#203437);
#12919=VERTEX_POINT('',#203438);
#12920=VERTEX_POINT('',#203674);
#12921=VERTEX_POINT('',#203913);
#12922=VERTEX_POINT('',#203914);
#12923=VERTEX_POINT('',#203916);
#12924=VERTEX_POINT('',#204152);
#12925=VERTEX_POINT('',#204348);
#12926=VERTEX_POINT('',#204509);
#12927=VERTEX_POINT('',#204618);
#12928=VERTEX_POINT('',#204779);
#12929=VERTEX_POINT('',#204888);
#12930=VERTEX_POINT('',#205049);
#12931=VERTEX_POINT('',#205158);
#12932=VERTEX_POINT('',#205319);
#12933=VERTEX_POINT('',#205428);
#12934=VERTEX_POINT('',#205447);
#12935=VERTEX_POINT('',#205463);
#12936=VERTEX_POINT('',#205500);
#12937=VERTEX_POINT('',#205508);
#12938=VERTEX_POINT('',#205567);
#12939=VERTEX_POINT('',#205569);
#12940=VERTEX_POINT('',#205582);
#12941=VERTEX_POINT('',#205590);
#12942=VERTEX_POINT('',#205649);
#12943=VERTEX_POINT('',#205651);
#12944=VERTEX_POINT('',#205664);
#12945=VERTEX_POINT('',#205672);
#12946=VERTEX_POINT('',#205731);
#12947=VERTEX_POINT('',#205733);
#12948=VERTEX_POINT('',#205746);
#12949=VERTEX_POINT('',#205754);
#12950=VERTEX_POINT('',#205813);
#12951=VERTEX_POINT('',#205815);
#12952=VERTEX_POINT('',#205828);
#12953=VERTEX_POINT('',#205835);
#12954=VERTEX_POINT('',#205990);
#12955=VERTEX_POINT('',#205992);
#12956=VERTEX_POINT('',#206048);
#12957=VERTEX_POINT('',#206055);
#12958=VERTEX_POINT('',#206210);
#12959=VERTEX_POINT('',#206212);
#12960=VERTEX_POINT('',#206268);
#12961=VERTEX_POINT('',#206270);
#12962=VERTEX_POINT('',#206275);
#12963=VERTEX_POINT('',#206276);
#12964=VERTEX_POINT('',#206278);
#12965=VERTEX_POINT('',#206280);
#12966=VERTEX_POINT('',#206284);
#12967=VERTEX_POINT('',#206286);
#12968=VERTEX_POINT('',#206288);
#12969=VERTEX_POINT('',#206292);
#12970=VERTEX_POINT('',#206294);
#12971=VERTEX_POINT('',#206299);
#12972=VERTEX_POINT('',#206300);
#12973=VERTEX_POINT('',#206302);
#12974=VERTEX_POINT('',#206304);
#12975=VERTEX_POINT('',#206308);
#12976=VERTEX_POINT('',#206309);
#12977=VERTEX_POINT('',#206311);
#12978=VERTEX_POINT('',#206316);
#12979=VERTEX_POINT('',#206318);
#12980=VERTEX_POINT('',#206323);
#12981=VERTEX_POINT('',#206325);
#12982=VERTEX_POINT('',#206329);
#12983=VERTEX_POINT('',#206331);
#12984=VERTEX_POINT('',#206333);
#12985=VERTEX_POINT('',#206337);
#12986=VERTEX_POINT('',#206342);
#12987=VERTEX_POINT('',#206344);
#12988=VERTEX_POINT('',#206346);
#12989=VERTEX_POINT('',#206348);
#12990=VERTEX_POINT('',#206350);
#12991=VERTEX_POINT('',#206352);
#12992=VERTEX_POINT('',#206354);
#12993=VERTEX_POINT('',#206356);
#12994=VERTEX_POINT('',#206358);
#12995=VERTEX_POINT('',#206360);
#12996=VERTEX_POINT('',#206362);
#12997=VERTEX_POINT('',#206364);
#12998=VERTEX_POINT('',#206366);
#12999=VERTEX_POINT('',#206368);
#13000=VERTEX_POINT('',#206370);
#13001=VERTEX_POINT('',#206372);
#13002=VERTEX_POINT('',#206374);
#13003=VERTEX_POINT('',#206376);
#13004=VERTEX_POINT('',#206378);
#13005=VERTEX_POINT('',#206380);
#13006=VERTEX_POINT('',#206382);
#13007=VERTEX_POINT('',#206384);
#13008=VERTEX_POINT('',#206386);
#13009=VERTEX_POINT('',#206388);
#13010=VERTEX_POINT('',#206390);
#13011=VERTEX_POINT('',#206392);
#13012=VERTEX_POINT('',#206394);
#13013=VERTEX_POINT('',#206397);
#13014=VERTEX_POINT('',#206399);
#13015=VERTEX_POINT('',#215197);
#13016=VERTEX_POINT('',#215198);
#13017=VERTEX_POINT('',#215200);
#13018=VERTEX_POINT('',#215202);
#13019=VERTEX_POINT('',#215206);
#13020=VERTEX_POINT('',#215208);
#13021=VERTEX_POINT('',#215212);
#13022=VERTEX_POINT('',#215214);
#13023=VERTEX_POINT('',#215218);
#13024=VERTEX_POINT('',#215220);
#13025=VERTEX_POINT('',#215224);
#13026=VERTEX_POINT('',#215226);
#13027=VERTEX_POINT('',#215230);
#13028=VERTEX_POINT('',#215232);
#13029=VERTEX_POINT('',#215239);
#13030=VERTEX_POINT('',#215241);
#13031=VERTEX_POINT('',#215246);
#13032=VERTEX_POINT('',#215247);
#13033=VERTEX_POINT('',#215249);
#13034=VERTEX_POINT('',#215251);
#13035=VERTEX_POINT('',#215255);
#13036=VERTEX_POINT('',#215257);
#13037=VERTEX_POINT('',#215261);
#13038=VERTEX_POINT('',#215263);
#13039=VERTEX_POINT('',#215273);
#13040=VERTEX_POINT('',#215275);
#13041=VERTEX_POINT('',#215278);
#13042=VERTEX_POINT('',#215279);
#13043=VERTEX_POINT('',#215281);
#13044=VERTEX_POINT('',#215283);
#13045=VERTEX_POINT('',#215287);
#13046=VERTEX_POINT('',#215289);
#13047=VERTEX_POINT('',#215293);
#13048=VERTEX_POINT('',#215295);
#13049=VERTEX_POINT('',#215299);
#13050=VERTEX_POINT('',#215301);
#13051=VERTEX_POINT('',#215305);
#13052=VERTEX_POINT('',#215307);
#13053=VERTEX_POINT('',#215311);
#13054=VERTEX_POINT('',#215313);
#13055=VERTEX_POINT('',#215320);
#13056=VERTEX_POINT('',#215322);
#13057=VERTEX_POINT('',#215329);
#13058=VERTEX_POINT('',#215335);
#13059=VERTEX_POINT('',#215340);
#13060=VERTEX_POINT('',#215341);
#13061=VERTEX_POINT('',#215343);
#13062=VERTEX_POINT('',#215345);
#13063=VERTEX_POINT('',#215349);
#13064=VERTEX_POINT('',#215351);
#13065=VERTEX_POINT('',#215355);
#13066=VERTEX_POINT('',#215357);
#13067=VERTEX_POINT('',#215367);
#13068=VERTEX_POINT('',#215369);
#13069=VERTEX_POINT('',#215372);
#13070=VERTEX_POINT('',#215373);
#13071=VERTEX_POINT('',#215375);
#13072=VERTEX_POINT('',#215377);
#13073=VERTEX_POINT('',#215381);
#13074=VERTEX_POINT('',#215383);
#13075=VERTEX_POINT('',#215387);
#13076=VERTEX_POINT('',#215389);
#13077=VERTEX_POINT('',#215393);
#13078=VERTEX_POINT('',#215395);
#13079=VERTEX_POINT('',#215399);
#13080=VERTEX_POINT('',#215401);
#13081=VERTEX_POINT('',#215405);
#13082=VERTEX_POINT('',#215407);
#13083=VERTEX_POINT('',#215414);
#13084=VERTEX_POINT('',#215416);
#13085=VERTEX_POINT('',#215421);
#13086=VERTEX_POINT('',#215422);
#13087=VERTEX_POINT('',#215424);
#13088=VERTEX_POINT('',#215426);
#13089=VERTEX_POINT('',#215430);
#13090=VERTEX_POINT('',#215432);
#13091=VERTEX_POINT('',#215436);
#13092=VERTEX_POINT('',#215438);
#13093=VERTEX_POINT('',#215442);
#13094=VERTEX_POINT('',#215444);
#13095=VERTEX_POINT('',#215448);
#13096=VERTEX_POINT('',#215450);
#13097=VERTEX_POINT('',#215454);
#13098=VERTEX_POINT('',#215456);
#13099=VERTEX_POINT('',#215463);
#13100=VERTEX_POINT('',#215465);
#13101=VERTEX_POINT('',#215472);
#13102=VERTEX_POINT('',#215474);
#13103=VERTEX_POINT('',#215479);
#13104=VERTEX_POINT('',#215484);
#13105=VERTEX_POINT('',#215489);
#13106=VERTEX_POINT('',#215494);
#13107=VERTEX_POINT('',#215499);
#13108=VERTEX_POINT('',#215505);
#13109=VERTEX_POINT('',#215509);
#13110=VERTEX_POINT('',#215513);
#13111=VERTEX_POINT('',#215517);
#13112=VERTEX_POINT('',#215521);
#13113=VERTEX_POINT('',#215525);
#13114=VERTEX_POINT('',#215531);
#13115=VERTEX_POINT('',#215535);
#13116=VERTEX_POINT('',#215539);
#13117=VERTEX_POINT('',#215543);
#13118=VERTEX_POINT('',#215547);
#13119=VERTEX_POINT('',#215551);
#13120=VERTEX_POINT('',#215555);
#13121=VERTEX_POINT('',#215559);
#13122=VERTEX_POINT('',#215563);
#13123=VERTEX_POINT('',#215567);
#13124=VERTEX_POINT('',#215571);
#13125=VERTEX_POINT('',#215575);
#16136=EDGE_CURVE('',#12072,#12073,#7722,.T.);
#16137=EDGE_CURVE('',#12074,#12072,#1233,.T.);
#16138=EDGE_CURVE('',#12074,#12075,#6208,.T.);
#16139=EDGE_CURVE('',#12075,#12073,#1234,.T.);
#16140=EDGE_CURVE('',#12076,#12077,#7723,.T.);
#16141=EDGE_CURVE('',#12078,#12076,#1235,.T.);
#16142=EDGE_CURVE('',#12072,#12078,#1236,.T.);
#16143=EDGE_CURVE('',#12073,#12079,#1237,.T.);
#16144=EDGE_CURVE('',#12079,#12077,#1238,.T.);
#16145=EDGE_CURVE('',#12080,#12081,#7724,.T.);
#16146=EDGE_CURVE('',#12082,#12080,#1239,.T.);
#16147=EDGE_CURVE('',#12076,#12082,#1240,.T.);
#16148=EDGE_CURVE('',#12077,#12083,#1241,.T.);
#16149=EDGE_CURVE('',#12083,#12081,#1242,.T.);
#16150=EDGE_CURVE('',#12084,#12085,#7725,.T.);
#16151=EDGE_CURVE('',#12086,#12084,#1243,.T.);
#16152=EDGE_CURVE('',#12080,#12086,#1244,.T.);
#16153=EDGE_CURVE('',#12081,#12087,#1245,.T.);
#16154=EDGE_CURVE('',#12087,#12085,#1246,.T.);
#16155=EDGE_CURVE('',#12088,#12089,#7726,.T.);
#16156=EDGE_CURVE('',#12090,#12088,#1247,.T.);
#16157=EDGE_CURVE('',#12090,#12091,#6209,.T.);
#16158=EDGE_CURVE('',#12091,#12089,#1248,.T.);
#16159=EDGE_CURVE('',#12092,#12093,#7727,.T.);
#16160=EDGE_CURVE('',#12094,#12092,#1249,.T.);
#16161=EDGE_CURVE('',#12088,#12094,#1250,.T.);
#16162=EDGE_CURVE('',#12089,#12095,#1251,.T.);
#16163=EDGE_CURVE('',#12095,#12093,#1252,.T.);
#16164=EDGE_CURVE('',#12096,#12097,#7728,.T.);
#16165=EDGE_CURVE('',#12098,#12096,#1253,.T.);
#16166=EDGE_CURVE('',#12092,#12098,#1254,.T.);
#16167=EDGE_CURVE('',#12093,#12099,#1255,.T.);
#16168=EDGE_CURVE('',#12099,#12097,#1256,.T.);
#16169=EDGE_CURVE('',#12100,#12101,#7729,.T.);
#16170=EDGE_CURVE('',#12102,#12100,#1257,.T.);
#16171=EDGE_CURVE('',#12096,#12102,#1258,.T.);
#16172=EDGE_CURVE('',#12097,#12103,#1259,.T.);
#16173=EDGE_CURVE('',#12103,#12101,#1260,.T.);
#16174=EDGE_CURVE('',#12104,#12105,#7730,.T.);
#16175=EDGE_CURVE('',#12106,#12104,#1261,.T.);
#16176=EDGE_CURVE('',#12107,#12106,#1262,.T.);
#16177=EDGE_CURVE('',#12107,#12108,#6210,.T.);
#16178=EDGE_CURVE('',#12108,#12109,#1263,.T.);
#16179=EDGE_CURVE('',#12109,#12105,#1264,.T.);
#16180=EDGE_CURVE('',#12110,#12111,#7731,.T.);
#16181=EDGE_CURVE('',#12112,#12110,#1265,.T.);
#16182=EDGE_CURVE('',#12104,#12112,#1266,.T.);
#16183=EDGE_CURVE('',#12105,#12113,#1267,.T.);
#16184=EDGE_CURVE('',#12113,#12111,#1268,.T.);
#16185=EDGE_CURVE('',#12114,#12115,#7732,.T.);
#16186=EDGE_CURVE('',#12116,#12114,#1269,.T.);
#16187=EDGE_CURVE('',#12110,#12116,#1270,.T.);
#16188=EDGE_CURVE('',#12111,#12117,#1271,.T.);
#16189=EDGE_CURVE('',#12117,#12115,#1272,.T.);
#16190=EDGE_CURVE('',#12118,#12119,#7733,.T.);
#16191=EDGE_CURVE('',#12120,#12118,#1273,.T.);
#16192=EDGE_CURVE('',#12114,#12120,#1274,.T.);
#16193=EDGE_CURVE('',#12115,#12121,#1275,.T.);
#16194=EDGE_CURVE('',#12121,#12119,#1276,.T.);
#16195=EDGE_CURVE('',#12122,#12123,#7734,.T.);
#16196=EDGE_CURVE('',#12124,#12122,#1277,.T.);
#16197=EDGE_CURVE('',#12118,#12124,#1278,.T.);
#16198=EDGE_CURVE('',#12119,#12125,#1279,.T.);
#16199=EDGE_CURVE('',#12125,#12123,#1280,.T.);
#16200=EDGE_CURVE('',#12126,#12127,#7735,.T.);
#16201=EDGE_CURVE('',#12128,#12126,#1281,.T.);
#16202=EDGE_CURVE('',#12122,#12128,#1282,.T.);
#16203=EDGE_CURVE('',#12123,#12129,#1283,.T.);
#16204=EDGE_CURVE('',#12129,#12127,#1284,.T.);
#16205=EDGE_CURVE('',#12130,#12131,#7736,.T.);
#16206=EDGE_CURVE('',#12132,#12130,#1285,.T.);
#16207=EDGE_CURVE('',#12126,#12132,#1286,.T.);
#16208=EDGE_CURVE('',#12127,#12133,#1287,.T.);
#16209=EDGE_CURVE('',#12133,#12131,#1288,.T.);
#16210=EDGE_CURVE('',#12134,#12135,#7737,.T.);
#16211=EDGE_CURVE('',#12136,#12134,#1289,.T.);
#16212=EDGE_CURVE('',#12130,#12136,#1290,.T.);
#16213=EDGE_CURVE('',#12131,#12137,#1291,.T.);
#16214=EDGE_CURVE('',#12137,#12135,#1292,.T.);
#16215=EDGE_CURVE('',#12138,#12139,#7738,.T.);
#16216=EDGE_CURVE('',#12140,#12138,#1293,.T.);
#16217=EDGE_CURVE('',#12134,#12140,#1294,.T.);
#16218=EDGE_CURVE('',#12135,#12141,#1295,.T.);
#16219=EDGE_CURVE('',#12141,#12139,#1296,.T.);
#16220=EDGE_CURVE('',#12142,#12143,#7739,.T.);
#16221=EDGE_CURVE('',#12144,#12142,#1297,.T.);
#16222=EDGE_CURVE('',#12138,#12144,#1298,.T.);
#16223=EDGE_CURVE('',#12139,#12145,#1299,.T.);
#16224=EDGE_CURVE('',#12145,#12143,#1300,.T.);
#16225=EDGE_CURVE('',#12146,#12147,#7740,.T.);
#16226=EDGE_CURVE('',#12148,#12146,#1301,.T.);
#16227=EDGE_CURVE('',#12142,#12148,#1302,.T.);
#16228=EDGE_CURVE('',#12143,#12149,#1303,.T.);
#16229=EDGE_CURVE('',#12149,#12147,#1304,.T.);
#16230=EDGE_CURVE('',#12150,#12151,#7741,.T.);
#16231=EDGE_CURVE('',#12152,#12150,#1305,.T.);
#16232=EDGE_CURVE('',#12146,#12152,#1306,.T.);
#16233=EDGE_CURVE('',#12147,#12153,#1307,.T.);
#16234=EDGE_CURVE('',#12153,#12151,#1308,.T.);
#16235=EDGE_CURVE('',#12154,#12155,#7742,.T.);
#16236=EDGE_CURVE('',#12156,#12154,#1309,.T.);
#16237=EDGE_CURVE('',#12150,#12156,#1310,.T.);
#16238=EDGE_CURVE('',#12151,#12157,#1311,.T.);
#16239=EDGE_CURVE('',#12157,#12155,#1312,.T.);
#16240=EDGE_CURVE('',#12158,#12159,#7743,.T.);
#16241=EDGE_CURVE('',#12160,#12158,#1313,.T.);
#16242=EDGE_CURVE('',#12154,#12160,#1314,.T.);
#16243=EDGE_CURVE('',#12155,#12161,#1315,.T.);
#16244=EDGE_CURVE('',#12161,#12159,#1316,.T.);
#16245=EDGE_CURVE('',#12162,#12163,#7744,.T.);
#16246=EDGE_CURVE('',#12164,#12162,#1317,.T.);
#16247=EDGE_CURVE('',#12158,#12164,#1318,.T.);
#16248=EDGE_CURVE('',#12159,#12165,#1319,.T.);
#16249=EDGE_CURVE('',#12165,#12163,#1320,.T.);
#16250=EDGE_CURVE('',#12166,#12167,#7745,.T.);
#16251=EDGE_CURVE('',#12168,#12166,#1321,.T.);
#16252=EDGE_CURVE('',#12162,#12168,#1322,.T.);
#16253=EDGE_CURVE('',#12163,#12169,#1323,.T.);
#16254=EDGE_CURVE('',#12169,#12167,#1324,.T.);
#16255=EDGE_CURVE('',#12170,#12171,#7746,.T.);
#16256=EDGE_CURVE('',#12172,#12170,#1325,.T.);
#16257=EDGE_CURVE('',#12166,#12172,#1326,.T.);
#16258=EDGE_CURVE('',#12167,#12173,#1327,.T.);
#16259=EDGE_CURVE('',#12173,#12171,#1328,.T.);
#16260=EDGE_CURVE('',#12174,#12175,#7747,.T.);
#16261=EDGE_CURVE('',#12176,#12174,#1329,.T.);
#16262=EDGE_CURVE('',#12170,#12176,#1330,.T.);
#16263=EDGE_CURVE('',#12171,#12177,#1331,.T.);
#16264=EDGE_CURVE('',#12177,#12175,#1332,.T.);
#16265=EDGE_CURVE('',#12178,#12179,#7748,.T.);
#16266=EDGE_CURVE('',#12180,#12178,#1333,.T.);
#16267=EDGE_CURVE('',#12174,#12180,#1334,.T.);
#16268=EDGE_CURVE('',#12175,#12181,#1335,.T.);
#16269=EDGE_CURVE('',#12181,#12179,#1336,.T.);
#16270=EDGE_CURVE('',#12182,#12183,#7749,.T.);
#16271=EDGE_CURVE('',#12184,#12182,#1337,.T.);
#16272=EDGE_CURVE('',#12178,#12184,#1338,.T.);
#16273=EDGE_CURVE('',#12179,#12185,#1339,.T.);
#16274=EDGE_CURVE('',#12185,#12183,#1340,.T.);
#16275=EDGE_CURVE('',#12186,#12187,#7750,.T.);
#16276=EDGE_CURVE('',#12188,#12186,#1341,.T.);
#16277=EDGE_CURVE('',#12182,#12188,#1342,.T.);
#16278=EDGE_CURVE('',#12183,#12189,#1343,.T.);
#16279=EDGE_CURVE('',#12189,#12187,#1344,.T.);
#16280=EDGE_CURVE('',#12190,#12191,#7751,.T.);
#16281=EDGE_CURVE('',#12192,#12190,#1345,.T.);
#16282=EDGE_CURVE('',#12186,#12192,#1346,.T.);
#16283=EDGE_CURVE('',#12187,#12193,#1347,.T.);
#16284=EDGE_CURVE('',#12193,#12191,#1348,.T.);
#16285=EDGE_CURVE('',#12194,#12195,#7752,.T.);
#16286=EDGE_CURVE('',#12196,#12194,#1349,.T.);
#16287=EDGE_CURVE('',#12190,#12196,#1350,.T.);
#16288=EDGE_CURVE('',#12191,#12197,#1351,.T.);
#16289=EDGE_CURVE('',#12197,#12195,#1352,.T.);
#16290=EDGE_CURVE('',#12198,#12199,#7753,.T.);
#16291=EDGE_CURVE('',#12200,#12198,#1353,.T.);
#16292=EDGE_CURVE('',#12194,#12200,#1354,.T.);
#16293=EDGE_CURVE('',#12195,#12201,#1355,.T.);
#16294=EDGE_CURVE('',#12201,#12199,#1356,.T.);
#16295=EDGE_CURVE('',#12202,#12203,#7754,.T.);
#16296=EDGE_CURVE('',#12204,#12202,#1357,.T.);
#16297=EDGE_CURVE('',#12198,#12204,#1358,.T.);
#16298=EDGE_CURVE('',#12199,#12205,#1359,.T.);
#16299=EDGE_CURVE('',#12205,#12203,#1360,.T.);
#16300=EDGE_CURVE('',#12206,#12207,#7755,.T.);
#16301=EDGE_CURVE('',#12208,#12206,#1361,.T.);
#16302=EDGE_CURVE('',#12202,#12208,#1362,.T.);
#16303=EDGE_CURVE('',#12203,#12209,#1363,.T.);
#16304=EDGE_CURVE('',#12209,#12207,#1364,.T.);
#16305=EDGE_CURVE('',#12210,#12211,#7756,.T.);
#16306=EDGE_CURVE('',#12212,#12210,#1365,.T.);
#16307=EDGE_CURVE('',#12206,#12212,#1366,.T.);
#16308=EDGE_CURVE('',#12207,#12213,#1367,.T.);
#16309=EDGE_CURVE('',#12213,#12211,#1368,.T.);
#16310=EDGE_CURVE('',#12214,#12215,#7757,.T.);
#16311=EDGE_CURVE('',#12216,#12214,#1369,.T.);
#16312=EDGE_CURVE('',#12217,#12216,#1370,.T.);
#16313=EDGE_CURVE('',#12217,#12218,#6211,.T.);
#16314=EDGE_CURVE('',#12218,#12219,#1371,.T.);
#16315=EDGE_CURVE('',#12219,#12215,#1372,.T.);
#16316=EDGE_CURVE('',#12220,#12221,#7758,.T.);
#16317=EDGE_CURVE('',#12222,#12220,#1373,.T.);
#16318=EDGE_CURVE('',#12214,#12222,#1374,.T.);
#16319=EDGE_CURVE('',#12215,#12223,#1375,.T.);
#16320=EDGE_CURVE('',#12223,#12221,#1376,.T.);
#16321=EDGE_CURVE('',#12224,#12225,#7759,.T.);
#16322=EDGE_CURVE('',#12226,#12224,#1377,.T.);
#16323=EDGE_CURVE('',#12220,#12226,#1378,.T.);
#16324=EDGE_CURVE('',#12221,#12227,#1379,.T.);
#16325=EDGE_CURVE('',#12227,#12225,#1380,.T.);
#16326=EDGE_CURVE('',#12228,#12229,#7760,.T.);
#16327=EDGE_CURVE('',#12230,#12228,#1381,.T.);
#16328=EDGE_CURVE('',#12224,#12230,#1382,.T.);
#16329=EDGE_CURVE('',#12225,#12231,#1383,.T.);
#16330=EDGE_CURVE('',#12231,#12229,#1384,.T.);
#16331=EDGE_CURVE('',#12232,#12233,#7761,.T.);
#16332=EDGE_CURVE('',#12234,#12232,#1385,.T.);
#16333=EDGE_CURVE('',#12228,#12234,#1386,.T.);
#16334=EDGE_CURVE('',#12229,#12235,#1387,.T.);
#16335=EDGE_CURVE('',#12235,#12233,#1388,.T.);
#16336=EDGE_CURVE('',#12236,#12237,#7762,.T.);
#16337=EDGE_CURVE('',#12238,#12236,#1389,.T.);
#16338=EDGE_CURVE('',#12232,#12238,#1390,.T.);
#16339=EDGE_CURVE('',#12233,#12239,#1391,.T.);
#16340=EDGE_CURVE('',#12239,#12237,#1392,.T.);
#16341=EDGE_CURVE('',#12240,#12241,#7763,.T.);
#16342=EDGE_CURVE('',#12242,#12240,#1393,.T.);
#16343=EDGE_CURVE('',#12236,#12242,#1394,.T.);
#16344=EDGE_CURVE('',#12237,#12243,#1395,.T.);
#16345=EDGE_CURVE('',#12243,#12241,#1396,.T.);
#16346=EDGE_CURVE('',#12244,#12245,#7764,.T.);
#16347=EDGE_CURVE('',#12246,#12244,#1397,.T.);
#16348=EDGE_CURVE('',#12240,#12246,#1398,.T.);
#16349=EDGE_CURVE('',#12241,#12247,#1399,.T.);
#16350=EDGE_CURVE('',#12247,#12245,#1400,.T.);
#16351=EDGE_CURVE('',#12248,#12249,#7765,.T.);
#16352=EDGE_CURVE('',#12250,#12248,#1401,.T.);
#16353=EDGE_CURVE('',#12244,#12250,#1402,.T.);
#16354=EDGE_CURVE('',#12245,#12251,#1403,.T.);
#16355=EDGE_CURVE('',#12251,#12249,#1404,.T.);
#16356=EDGE_CURVE('',#12252,#12253,#7766,.T.);
#16357=EDGE_CURVE('',#12254,#12252,#1405,.T.);
#16358=EDGE_CURVE('',#12248,#12254,#1406,.T.);
#16359=EDGE_CURVE('',#12249,#12255,#1407,.T.);
#16360=EDGE_CURVE('',#12255,#12253,#1408,.T.);
#16361=EDGE_CURVE('',#12256,#12257,#7767,.T.);
#16362=EDGE_CURVE('',#12258,#12256,#1409,.T.);
#16363=EDGE_CURVE('',#12252,#12258,#1410,.T.);
#16364=EDGE_CURVE('',#12253,#12259,#1411,.T.);
#16365=EDGE_CURVE('',#12259,#12257,#1412,.T.);
#16366=EDGE_CURVE('',#12260,#12261,#7768,.T.);
#16367=EDGE_CURVE('',#12262,#12260,#1413,.T.);
#16368=EDGE_CURVE('',#12256,#12262,#1414,.T.);
#16369=EDGE_CURVE('',#12257,#12263,#1415,.T.);
#16370=EDGE_CURVE('',#12263,#12261,#1416,.T.);
#16371=EDGE_CURVE('',#12264,#12265,#7769,.T.);
#16372=EDGE_CURVE('',#12266,#12264,#1417,.T.);
#16373=EDGE_CURVE('',#12260,#12266,#1418,.T.);
#16374=EDGE_CURVE('',#12261,#12267,#1419,.T.);
#16375=EDGE_CURVE('',#12267,#12265,#1420,.T.);
#16376=EDGE_CURVE('',#12268,#12269,#7770,.T.);
#16377=EDGE_CURVE('',#12270,#12268,#1421,.T.);
#16378=EDGE_CURVE('',#12264,#12270,#1422,.T.);
#16379=EDGE_CURVE('',#12265,#12271,#1423,.T.);
#16380=EDGE_CURVE('',#12271,#12269,#1424,.T.);
#16381=EDGE_CURVE('',#12272,#12273,#7771,.T.);
#16382=EDGE_CURVE('',#12274,#12272,#1425,.T.);
#16383=EDGE_CURVE('',#12268,#12274,#1426,.T.);
#16384=EDGE_CURVE('',#12269,#12275,#1427,.T.);
#16385=EDGE_CURVE('',#12275,#12273,#1428,.T.);
#16386=EDGE_CURVE('',#12276,#12277,#7772,.T.);
#16387=EDGE_CURVE('',#12278,#12276,#1429,.T.);
#16388=EDGE_CURVE('',#12272,#12278,#1430,.T.);
#16389=EDGE_CURVE('',#12273,#12279,#1431,.T.);
#16390=EDGE_CURVE('',#12279,#12277,#1432,.T.);
#16391=EDGE_CURVE('',#12280,#12281,#7773,.T.);
#16392=EDGE_CURVE('',#12282,#12280,#1433,.T.);
#16393=EDGE_CURVE('',#12276,#12282,#1434,.T.);
#16394=EDGE_CURVE('',#12277,#12283,#1435,.T.);
#16395=EDGE_CURVE('',#12283,#12281,#1436,.T.);
#16396=EDGE_CURVE('',#12284,#12285,#7774,.T.);
#16397=EDGE_CURVE('',#12286,#12284,#1437,.T.);
#16398=EDGE_CURVE('',#12280,#12286,#1438,.T.);
#16399=EDGE_CURVE('',#12281,#12287,#1439,.T.);
#16400=EDGE_CURVE('',#12287,#12285,#1440,.T.);
#16401=EDGE_CURVE('',#12288,#12289,#7775,.T.);
#16402=EDGE_CURVE('',#12290,#12288,#1441,.T.);
#16403=EDGE_CURVE('',#12284,#12290,#1442,.T.);
#16404=EDGE_CURVE('',#12285,#12291,#1443,.T.);
#16405=EDGE_CURVE('',#12291,#12289,#1444,.T.);
#16406=EDGE_CURVE('',#12292,#12293,#7776,.T.);
#16407=EDGE_CURVE('',#12294,#12292,#1445,.T.);
#16408=EDGE_CURVE('',#12288,#12294,#1446,.T.);
#16409=EDGE_CURVE('',#12289,#12295,#1447,.T.);
#16410=EDGE_CURVE('',#12295,#12293,#1448,.T.);
#16411=EDGE_CURVE('',#12296,#12297,#7777,.T.);
#16412=EDGE_CURVE('',#12298,#12296,#1449,.T.);
#16413=EDGE_CURVE('',#12292,#12298,#1450,.T.);
#16414=EDGE_CURVE('',#12293,#12299,#1451,.T.);
#16415=EDGE_CURVE('',#12299,#12297,#1452,.T.);
#16416=EDGE_CURVE('',#12300,#12301,#7778,.T.);
#16417=EDGE_CURVE('',#12302,#12300,#1453,.T.);
#16418=EDGE_CURVE('',#12296,#12302,#1454,.T.);
#16419=EDGE_CURVE('',#12297,#12303,#1455,.T.);
#16420=EDGE_CURVE('',#12303,#12301,#1456,.T.);
#16421=EDGE_CURVE('',#12304,#12305,#7779,.T.);
#16422=EDGE_CURVE('',#12306,#12304,#1457,.T.);
#16423=EDGE_CURVE('',#12300,#12306,#1458,.T.);
#16424=EDGE_CURVE('',#12301,#12307,#1459,.T.);
#16425=EDGE_CURVE('',#12307,#12305,#1460,.T.);
#16426=EDGE_CURVE('',#12308,#12309,#7780,.T.);
#16427=EDGE_CURVE('',#12310,#12308,#1461,.T.);
#16428=EDGE_CURVE('',#12304,#12310,#1462,.T.);
#16429=EDGE_CURVE('',#12305,#12311,#1463,.T.);
#16430=EDGE_CURVE('',#12311,#12309,#1464,.T.);
#16431=EDGE_CURVE('',#12312,#12313,#7781,.T.);
#16432=EDGE_CURVE('',#12314,#12312,#1465,.T.);
#16433=EDGE_CURVE('',#12308,#12314,#1466,.T.);
#16434=EDGE_CURVE('',#12309,#12315,#1467,.T.);
#16435=EDGE_CURVE('',#12315,#12313,#1468,.T.);
#16436=EDGE_CURVE('',#12316,#12317,#7782,.T.);
#16437=EDGE_CURVE('',#12318,#12316,#1469,.T.);
#16438=EDGE_CURVE('',#12312,#12318,#1470,.T.);
#16439=EDGE_CURVE('',#12313,#12319,#1471,.T.);
#16440=EDGE_CURVE('',#12319,#12317,#1472,.T.);
#16441=EDGE_CURVE('',#12320,#12321,#7783,.T.);
#16442=EDGE_CURVE('',#12322,#12320,#1473,.T.);
#16443=EDGE_CURVE('',#12316,#12322,#1474,.T.);
#16444=EDGE_CURVE('',#12317,#12323,#1475,.T.);
#16445=EDGE_CURVE('',#12323,#12321,#1476,.T.);
#16446=EDGE_CURVE('',#12324,#12325,#7784,.T.);
#16447=EDGE_CURVE('',#12326,#12324,#1477,.T.);
#16448=EDGE_CURVE('',#12327,#12326,#1478,.T.);
#16449=EDGE_CURVE('',#12327,#12328,#6212,.T.);
#16450=EDGE_CURVE('',#12328,#12329,#1479,.T.);
#16451=EDGE_CURVE('',#12329,#12325,#1480,.T.);
#16452=EDGE_CURVE('',#12330,#12331,#7785,.T.);
#16453=EDGE_CURVE('',#12332,#12330,#1481,.T.);
#16454=EDGE_CURVE('',#12324,#12332,#1482,.T.);
#16455=EDGE_CURVE('',#12325,#12333,#1483,.T.);
#16456=EDGE_CURVE('',#12333,#12331,#1484,.T.);
#16457=EDGE_CURVE('',#12334,#12335,#7786,.T.);
#16458=EDGE_CURVE('',#12336,#12334,#1485,.T.);
#16459=EDGE_CURVE('',#12330,#12336,#1486,.T.);
#16460=EDGE_CURVE('',#12331,#12337,#1487,.T.);
#16461=EDGE_CURVE('',#12337,#12335,#1488,.T.);
#16462=EDGE_CURVE('',#12338,#12339,#7787,.T.);
#16463=EDGE_CURVE('',#12340,#12338,#1489,.T.);
#16464=EDGE_CURVE('',#12334,#12340,#1490,.T.);
#16465=EDGE_CURVE('',#12335,#12341,#1491,.T.);
#16466=EDGE_CURVE('',#12341,#12339,#1492,.T.);
#16467=EDGE_CURVE('',#12342,#12343,#7788,.T.);
#16468=EDGE_CURVE('',#12344,#12342,#1493,.T.);
#16469=EDGE_CURVE('',#12338,#12344,#1494,.T.);
#16470=EDGE_CURVE('',#12339,#12345,#1495,.T.);
#16471=EDGE_CURVE('',#12345,#12343,#1496,.T.);
#16472=EDGE_CURVE('',#12346,#12347,#7789,.T.);
#16473=EDGE_CURVE('',#12348,#12346,#1497,.T.);
#16474=EDGE_CURVE('',#12342,#12348,#1498,.T.);
#16475=EDGE_CURVE('',#12343,#12349,#1499,.T.);
#16476=EDGE_CURVE('',#12349,#12347,#1500,.T.);
#16477=EDGE_CURVE('',#12350,#12351,#7790,.T.);
#16478=EDGE_CURVE('',#12352,#12350,#1501,.T.);
#16479=EDGE_CURVE('',#12346,#12352,#1502,.T.);
#16480=EDGE_CURVE('',#12347,#12353,#1503,.T.);
#16481=EDGE_CURVE('',#12353,#12351,#1504,.T.);
#16482=EDGE_CURVE('',#12354,#12355,#7791,.T.);
#16483=EDGE_CURVE('',#12356,#12354,#1505,.T.);
#16484=EDGE_CURVE('',#12350,#12356,#1506,.T.);
#16485=EDGE_CURVE('',#12351,#12357,#1507,.T.);
#16486=EDGE_CURVE('',#12357,#12355,#1508,.T.);
#16487=EDGE_CURVE('',#12358,#12359,#7792,.T.);
#16488=EDGE_CURVE('',#12360,#12358,#1509,.T.);
#16489=EDGE_CURVE('',#12354,#12360,#1510,.T.);
#16490=EDGE_CURVE('',#12355,#12361,#1511,.T.);
#16491=EDGE_CURVE('',#12361,#12359,#1512,.T.);
#16492=EDGE_CURVE('',#12362,#12363,#7793,.T.);
#16493=EDGE_CURVE('',#12364,#12362,#1513,.T.);
#16494=EDGE_CURVE('',#12358,#12364,#1514,.T.);
#16495=EDGE_CURVE('',#12359,#12365,#1515,.T.);
#16496=EDGE_CURVE('',#12365,#12363,#1516,.T.);
#16497=EDGE_CURVE('',#12366,#12367,#7794,.T.);
#16498=EDGE_CURVE('',#12368,#12366,#1517,.T.);
#16499=EDGE_CURVE('',#12362,#12368,#1518,.T.);
#16500=EDGE_CURVE('',#12363,#12369,#1519,.T.);
#16501=EDGE_CURVE('',#12369,#12367,#1520,.T.);
#16502=EDGE_CURVE('',#12370,#12371,#7795,.T.);
#16503=EDGE_CURVE('',#12372,#12370,#1521,.T.);
#16504=EDGE_CURVE('',#12366,#12372,#1522,.T.);
#16505=EDGE_CURVE('',#12367,#12373,#1523,.T.);
#16506=EDGE_CURVE('',#12373,#12371,#1524,.T.);
#16507=EDGE_CURVE('',#12374,#12375,#7796,.T.);
#16508=EDGE_CURVE('',#12376,#12374,#1525,.T.);
#16509=EDGE_CURVE('',#12370,#12376,#1526,.T.);
#16510=EDGE_CURVE('',#12371,#12377,#1527,.T.);
#16511=EDGE_CURVE('',#12377,#12375,#1528,.T.);
#16512=EDGE_CURVE('',#12378,#12379,#7797,.T.);
#16513=EDGE_CURVE('',#12380,#12378,#1529,.T.);
#16514=EDGE_CURVE('',#12374,#12380,#1530,.T.);
#16515=EDGE_CURVE('',#12375,#12381,#1531,.T.);
#16516=EDGE_CURVE('',#12381,#12379,#1532,.T.);
#16517=EDGE_CURVE('',#12382,#12383,#7798,.T.);
#16518=EDGE_CURVE('',#12384,#12382,#1533,.T.);
#16519=EDGE_CURVE('',#12378,#12384,#1534,.T.);
#16520=EDGE_CURVE('',#12379,#12385,#1535,.T.);
#16521=EDGE_CURVE('',#12385,#12383,#1536,.T.);
#16522=EDGE_CURVE('',#12386,#12387,#7799,.T.);
#16523=EDGE_CURVE('',#12388,#12386,#1537,.T.);
#16524=EDGE_CURVE('',#12382,#12388,#1538,.T.);
#16525=EDGE_CURVE('',#12383,#12389,#1539,.T.);
#16526=EDGE_CURVE('',#12389,#12387,#1540,.T.);
#16527=EDGE_CURVE('',#12390,#12391,#7800,.T.);
#16528=EDGE_CURVE('',#12392,#12390,#1541,.T.);
#16529=EDGE_CURVE('',#12386,#12392,#1542,.T.);
#16530=EDGE_CURVE('',#12387,#12393,#1543,.T.);
#16531=EDGE_CURVE('',#12393,#12391,#1544,.T.);
#16532=EDGE_CURVE('',#12394,#12395,#7801,.T.);
#16533=EDGE_CURVE('',#12396,#12394,#1545,.T.);
#16534=EDGE_CURVE('',#12390,#12396,#1546,.T.);
#16535=EDGE_CURVE('',#12391,#12397,#1547,.T.);
#16536=EDGE_CURVE('',#12397,#12395,#1548,.T.);
#16537=EDGE_CURVE('',#12398,#12399,#7802,.T.);
#16538=EDGE_CURVE('',#12400,#12398,#1549,.T.);
#16539=EDGE_CURVE('',#12394,#12400,#1550,.T.);
#16540=EDGE_CURVE('',#12395,#12401,#1551,.T.);
#16541=EDGE_CURVE('',#12401,#12399,#1552,.T.);
#16542=EDGE_CURVE('',#12402,#12403,#7803,.T.);
#16543=EDGE_CURVE('',#12404,#12402,#1553,.T.);
#16544=EDGE_CURVE('',#12398,#12404,#1554,.T.);
#16545=EDGE_CURVE('',#12399,#12405,#1555,.T.);
#16546=EDGE_CURVE('',#12405,#12403,#1556,.T.);
#16547=EDGE_CURVE('',#12406,#12407,#7804,.T.);
#16548=EDGE_CURVE('',#12408,#12406,#1557,.T.);
#16549=EDGE_CURVE('',#12402,#12408,#1558,.T.);
#16550=EDGE_CURVE('',#12403,#12409,#1559,.T.);
#16551=EDGE_CURVE('',#12409,#12407,#1560,.T.);
#16552=EDGE_CURVE('',#12410,#12411,#7805,.T.);
#16553=EDGE_CURVE('',#12412,#12410,#1561,.T.);
#16554=EDGE_CURVE('',#12406,#12412,#1562,.T.);
#16555=EDGE_CURVE('',#12407,#12413,#1563,.T.);
#16556=EDGE_CURVE('',#12413,#12411,#1564,.T.);
#16557=EDGE_CURVE('',#12414,#12415,#7806,.T.);
#16558=EDGE_CURVE('',#12416,#12414,#1565,.T.);
#16559=EDGE_CURVE('',#12410,#12416,#1566,.T.);
#16560=EDGE_CURVE('',#12411,#12417,#1567,.T.);
#16561=EDGE_CURVE('',#12417,#12415,#1568,.T.);
#16562=EDGE_CURVE('',#12418,#12419,#7807,.T.);
#16563=EDGE_CURVE('',#12420,#12418,#1569,.T.);
#16564=EDGE_CURVE('',#12414,#12420,#1570,.T.);
#16565=EDGE_CURVE('',#12415,#12421,#1571,.T.);
#16566=EDGE_CURVE('',#12421,#12419,#1572,.T.);
#16567=EDGE_CURVE('',#12422,#12423,#7808,.T.);
#16568=EDGE_CURVE('',#12424,#12422,#1573,.T.);
#16569=EDGE_CURVE('',#12418,#12424,#1574,.T.);
#16570=EDGE_CURVE('',#12419,#12425,#1575,.T.);
#16571=EDGE_CURVE('',#12425,#12423,#1576,.T.);
#16572=EDGE_CURVE('',#12426,#12427,#7809,.T.);
#16573=EDGE_CURVE('',#12428,#12426,#1577,.T.);
#16574=EDGE_CURVE('',#12422,#12428,#1578,.T.);
#16575=EDGE_CURVE('',#12423,#12429,#1579,.T.);
#16576=EDGE_CURVE('',#12429,#12427,#1580,.T.);
#16577=EDGE_CURVE('',#12430,#12431,#7810,.T.);
#16578=EDGE_CURVE('',#12432,#12430,#1581,.T.);
#16579=EDGE_CURVE('',#12426,#12432,#1582,.T.);
#16580=EDGE_CURVE('',#12427,#12433,#1583,.T.);
#16581=EDGE_CURVE('',#12433,#12431,#1584,.T.);
#16582=EDGE_CURVE('',#12434,#12435,#7811,.T.);
#16583=EDGE_CURVE('',#12436,#12434,#1585,.T.);
#16584=EDGE_CURVE('',#12437,#12436,#1586,.T.);
#16585=EDGE_CURVE('',#12437,#12438,#6213,.T.);
#16586=EDGE_CURVE('',#12438,#12439,#1587,.T.);
#16587=EDGE_CURVE('',#12439,#12435,#1588,.T.);
#16588=EDGE_CURVE('',#12440,#12441,#7812,.T.);
#16589=EDGE_CURVE('',#12442,#12440,#1589,.T.);
#16590=EDGE_CURVE('',#12434,#12442,#1590,.T.);
#16591=EDGE_CURVE('',#12435,#12443,#1591,.T.);
#16592=EDGE_CURVE('',#12443,#12441,#1592,.T.);
#16593=EDGE_CURVE('',#12444,#12445,#7813,.T.);
#16594=EDGE_CURVE('',#12446,#12444,#1593,.T.);
#16595=EDGE_CURVE('',#12440,#12446,#1594,.T.);
#16596=EDGE_CURVE('',#12441,#12447,#1595,.T.);
#16597=EDGE_CURVE('',#12447,#12445,#1596,.T.);
#16598=EDGE_CURVE('',#12448,#12449,#7814,.T.);
#16599=EDGE_CURVE('',#12450,#12448,#1597,.T.);
#16600=EDGE_CURVE('',#12444,#12450,#1598,.T.);
#16601=EDGE_CURVE('',#12445,#12451,#1599,.T.);
#16602=EDGE_CURVE('',#12451,#12449,#1600,.T.);
#16603=EDGE_CURVE('',#12452,#12453,#7815,.T.);
#16604=EDGE_CURVE('',#12454,#12452,#1601,.T.);
#16605=EDGE_CURVE('',#12448,#12454,#1602,.T.);
#16606=EDGE_CURVE('',#12449,#12455,#1603,.T.);
#16607=EDGE_CURVE('',#12455,#12453,#1604,.T.);
#16608=EDGE_CURVE('',#12456,#12457,#7816,.T.);
#16609=EDGE_CURVE('',#12458,#12456,#1605,.T.);
#16610=EDGE_CURVE('',#12452,#12458,#1606,.T.);
#16611=EDGE_CURVE('',#12453,#12459,#1607,.T.);
#16612=EDGE_CURVE('',#12459,#12457,#1608,.T.);
#16613=EDGE_CURVE('',#12460,#12461,#7817,.T.);
#16614=EDGE_CURVE('',#12462,#12460,#1609,.T.);
#16615=EDGE_CURVE('',#12456,#12462,#1610,.T.);
#16616=EDGE_CURVE('',#12457,#12463,#1611,.T.);
#16617=EDGE_CURVE('',#12463,#12461,#1612,.T.);
#16618=EDGE_CURVE('',#12464,#12465,#7818,.T.);
#16619=EDGE_CURVE('',#12466,#12464,#1613,.T.);
#16620=EDGE_CURVE('',#12460,#12466,#1614,.T.);
#16621=EDGE_CURVE('',#12461,#12467,#1615,.T.);
#16622=EDGE_CURVE('',#12467,#12465,#1616,.T.);
#16623=EDGE_CURVE('',#12468,#12469,#7819,.T.);
#16624=EDGE_CURVE('',#12470,#12468,#1617,.T.);
#16625=EDGE_CURVE('',#12464,#12470,#1618,.T.);
#16626=EDGE_CURVE('',#12465,#12471,#1619,.T.);
#16627=EDGE_CURVE('',#12471,#12469,#1620,.T.);
#16628=EDGE_CURVE('',#12472,#12473,#7820,.T.);
#16629=EDGE_CURVE('',#12474,#12472,#1621,.T.);
#16630=EDGE_CURVE('',#12468,#12474,#1622,.T.);
#16631=EDGE_CURVE('',#12469,#12475,#1623,.T.);
#16632=EDGE_CURVE('',#12475,#12473,#1624,.T.);
#16633=EDGE_CURVE('',#12476,#12477,#7821,.T.);
#16634=EDGE_CURVE('',#12478,#12476,#1625,.T.);
#16635=EDGE_CURVE('',#12472,#12478,#1626,.T.);
#16636=EDGE_CURVE('',#12473,#12479,#1627,.T.);
#16637=EDGE_CURVE('',#12479,#12477,#1628,.T.);
#16638=EDGE_CURVE('',#12480,#12481,#7822,.T.);
#16639=EDGE_CURVE('',#12482,#12480,#1629,.T.);
#16640=EDGE_CURVE('',#12476,#12482,#1630,.T.);
#16641=EDGE_CURVE('',#12477,#12483,#1631,.T.);
#16642=EDGE_CURVE('',#12483,#12481,#1632,.T.);
#16643=EDGE_CURVE('',#12484,#12485,#7823,.T.);
#16644=EDGE_CURVE('',#12486,#12484,#1633,.T.);
#16645=EDGE_CURVE('',#12480,#12486,#1634,.T.);
#16646=EDGE_CURVE('',#12481,#12487,#1635,.T.);
#16647=EDGE_CURVE('',#12487,#12485,#1636,.T.);
#16648=EDGE_CURVE('',#12488,#12489,#7824,.T.);
#16649=EDGE_CURVE('',#12490,#12488,#1637,.T.);
#16650=EDGE_CURVE('',#12484,#12490,#1638,.T.);
#16651=EDGE_CURVE('',#12485,#12491,#1639,.T.);
#16652=EDGE_CURVE('',#12491,#12489,#1640,.T.);
#16653=EDGE_CURVE('',#12492,#12493,#7825,.T.);
#16654=EDGE_CURVE('',#12494,#12492,#1641,.T.);
#16655=EDGE_CURVE('',#12488,#12494,#1642,.T.);
#16656=EDGE_CURVE('',#12489,#12495,#1643,.T.);
#16657=EDGE_CURVE('',#12495,#12493,#1644,.T.);
#16658=EDGE_CURVE('',#12496,#12497,#7826,.T.);
#16659=EDGE_CURVE('',#12498,#12496,#1645,.T.);
#16660=EDGE_CURVE('',#12492,#12498,#1646,.T.);
#16661=EDGE_CURVE('',#12493,#12499,#1647,.T.);
#16662=EDGE_CURVE('',#12499,#12497,#1648,.T.);
#16663=EDGE_CURVE('',#12500,#12501,#7827,.T.);
#16664=EDGE_CURVE('',#12502,#12500,#1649,.T.);
#16665=EDGE_CURVE('',#12496,#12502,#1650,.T.);
#16666=EDGE_CURVE('',#12497,#12503,#1651,.T.);
#16667=EDGE_CURVE('',#12503,#12501,#1652,.T.);
#16668=EDGE_CURVE('',#12504,#12505,#7828,.T.);
#16669=EDGE_CURVE('',#12506,#12504,#1653,.T.);
#16670=EDGE_CURVE('',#12500,#12506,#1654,.T.);
#16671=EDGE_CURVE('',#12501,#12507,#1655,.T.);
#16672=EDGE_CURVE('',#12507,#12505,#1656,.T.);
#16673=EDGE_CURVE('',#12508,#12509,#7829,.T.);
#16674=EDGE_CURVE('',#12510,#12508,#1657,.T.);
#16675=EDGE_CURVE('',#12504,#12510,#1658,.T.);
#16676=EDGE_CURVE('',#12505,#12511,#1659,.T.);
#16677=EDGE_CURVE('',#12511,#12509,#1660,.T.);
#16678=EDGE_CURVE('',#12512,#12513,#7830,.T.);
#16679=EDGE_CURVE('',#12514,#12512,#1661,.T.);
#16680=EDGE_CURVE('',#12508,#12514,#1662,.T.);
#16681=EDGE_CURVE('',#12509,#12515,#1663,.T.);
#16682=EDGE_CURVE('',#12515,#12513,#1664,.T.);
#16683=EDGE_CURVE('',#12516,#12517,#7831,.T.);
#16684=EDGE_CURVE('',#12518,#12516,#1665,.T.);
#16685=EDGE_CURVE('',#12512,#12518,#1666,.T.);
#16686=EDGE_CURVE('',#12513,#12519,#1667,.T.);
#16687=EDGE_CURVE('',#12519,#12517,#1668,.T.);
#16688=EDGE_CURVE('',#12520,#12521,#7832,.T.);
#16689=EDGE_CURVE('',#12522,#12520,#1669,.T.);
#16690=EDGE_CURVE('',#12516,#12522,#1670,.T.);
#16691=EDGE_CURVE('',#12517,#12523,#1671,.T.);
#16692=EDGE_CURVE('',#12523,#12521,#1672,.T.);
#16693=EDGE_CURVE('',#12524,#12525,#7833,.T.);
#16694=EDGE_CURVE('',#12526,#12524,#1673,.T.);
#16695=EDGE_CURVE('',#12520,#12526,#1674,.T.);
#16696=EDGE_CURVE('',#12521,#12527,#1675,.T.);
#16697=EDGE_CURVE('',#12527,#12525,#1676,.T.);
#16698=EDGE_CURVE('',#12528,#12529,#7834,.T.);
#16699=EDGE_CURVE('',#12530,#12528,#1677,.T.);
#16700=EDGE_CURVE('',#12524,#12530,#1678,.T.);
#16701=EDGE_CURVE('',#12525,#12531,#1679,.T.);
#16702=EDGE_CURVE('',#12531,#12529,#1680,.T.);
#16703=EDGE_CURVE('',#12532,#12533,#7835,.T.);
#16704=EDGE_CURVE('',#12534,#12532,#1681,.T.);
#16705=EDGE_CURVE('',#12528,#12534,#1682,.T.);
#16706=EDGE_CURVE('',#12529,#12535,#1683,.T.);
#16707=EDGE_CURVE('',#12535,#12533,#1684,.T.);
#16708=EDGE_CURVE('',#12536,#12537,#7836,.T.);
#16709=EDGE_CURVE('',#12538,#12536,#1685,.T.);
#16710=EDGE_CURVE('',#12532,#12538,#1686,.T.);
#16711=EDGE_CURVE('',#12533,#12539,#1687,.T.);
#16712=EDGE_CURVE('',#12539,#12537,#1688,.T.);
#16713=EDGE_CURVE('',#12540,#12541,#7837,.T.);
#16714=EDGE_CURVE('',#12542,#12540,#1689,.T.);
#16715=EDGE_CURVE('',#12536,#12542,#1690,.T.);
#16716=EDGE_CURVE('',#12537,#12543,#1691,.T.);
#16717=EDGE_CURVE('',#12543,#12541,#1692,.T.);
#16718=EDGE_CURVE('',#12544,#12545,#7838,.T.);
#16719=EDGE_CURVE('',#12546,#12544,#1693,.T.);
#16720=EDGE_CURVE('',#12546,#12545,#6214,.F.);
#16721=EDGE_CURVE('',#12547,#12548,#7839,.T.);
#16722=EDGE_CURVE('',#12544,#12547,#1694,.T.);
#16723=EDGE_CURVE('',#12545,#12549,#6215,.F.);
#16724=EDGE_CURVE('',#12548,#12549,#1695,.F.);
#16725=EDGE_CURVE('',#12550,#12551,#7840,.T.);
#16726=EDGE_CURVE('',#12547,#12550,#1696,.T.);
#16727=EDGE_CURVE('',#12551,#12548,#1697,.F.);
#16728=EDGE_CURVE('',#12552,#12553,#7841,.T.);
#16729=EDGE_CURVE('',#12550,#12552,#1698,.F.);
#16730=EDGE_CURVE('',#12553,#12551,#1699,.T.);
#16731=EDGE_CURVE('',#12554,#12555,#7842,.T.);
#16732=EDGE_CURVE('',#12556,#12554,#1700,.T.);
#16733=EDGE_CURVE('',#12557,#12556,#6216,.F.);
#16734=EDGE_CURVE('',#12555,#12557,#1701,.F.);
#16735=EDGE_CURVE('',#12558,#12559,#7843,.T.);
#16736=EDGE_CURVE('',#12554,#12558,#1702,.T.);
#16737=EDGE_CURVE('',#12559,#12555,#1703,.F.);
#16738=EDGE_CURVE('',#12560,#12561,#7844,.T.);
#16739=EDGE_CURVE('',#12558,#12560,#1704,.F.);
#16740=EDGE_CURVE('',#12561,#12559,#1705,.T.);
#16741=EDGE_CURVE('',#12562,#12563,#7845,.T.);
#16742=EDGE_CURVE('',#12564,#12562,#6217,.T.);
#16743=EDGE_CURVE('',#12560,#12564,#1706,.F.);
#16744=EDGE_CURVE('',#12563,#12561,#1707,.T.);
#16745=EDGE_CURVE('',#12565,#12566,#7846,.T.);
#16746=EDGE_CURVE('',#12567,#12565,#1708,.T.);
#16747=EDGE_CURVE('',#12568,#12567,#1709,.T.);
#16748=EDGE_CURVE('',#12568,#12569,#6218,.F.);
#16749=EDGE_CURVE('',#12570,#12569,#1710,.T.);
#16750=EDGE_CURVE('',#12566,#12570,#1711,.F.);
#16751=EDGE_CURVE('',#12571,#12572,#7847,.T.);
#16752=EDGE_CURVE('',#12573,#12571,#1712,.F.);
#16753=EDGE_CURVE('',#12565,#12573,#1713,.T.);
#16754=EDGE_CURVE('',#12572,#12566,#1714,.F.);
#16755=EDGE_CURVE('',#12574,#12575,#7848,.T.);
#16756=EDGE_CURVE('',#12571,#12574,#1715,.F.);
#16757=EDGE_CURVE('',#12576,#12572,#1716,.F.);
#16758=EDGE_CURVE('',#12575,#12576,#1717,.T.);
#16759=EDGE_CURVE('',#12577,#12578,#7849,.T.);
#16760=EDGE_CURVE('',#12579,#12577,#1718,.F.);
#16761=EDGE_CURVE('',#12574,#12579,#1719,.F.);
#16762=EDGE_CURVE('',#12580,#12575,#1720,.T.);
#16763=EDGE_CURVE('',#12578,#12580,#1721,.F.);
#16764=EDGE_CURVE('',#12581,#12582,#7850,.T.);
#16765=EDGE_CURVE('',#12577,#12581,#1722,.F.);
#16766=EDGE_CURVE('',#12582,#12578,#1723,.F.);
#16767=EDGE_CURVE('',#12583,#12584,#7851,.T.);
#16768=EDGE_CURVE('',#12585,#12583,#1724,.F.);
#16769=EDGE_CURVE('',#12581,#12585,#1725,.F.);
#16770=EDGE_CURVE('',#12586,#12582,#1726,.F.);
#16771=EDGE_CURVE('',#12584,#12586,#1727,.F.);
#16772=EDGE_CURVE('',#12587,#12588,#7852,.T.);
#16773=EDGE_CURVE('',#12583,#12587,#1728,.F.);
#16774=EDGE_CURVE('',#12588,#12584,#1729,.F.);
#16775=EDGE_CURVE('',#12589,#12590,#7853,.T.);
#16776=EDGE_CURVE('',#12591,#12589,#1730,.F.);
#16777=EDGE_CURVE('',#12587,#12591,#1731,.F.);
#16778=EDGE_CURVE('',#12592,#12588,#1732,.F.);
#16779=EDGE_CURVE('',#12590,#12592,#1733,.T.);
#16780=EDGE_CURVE('',#12593,#12594,#7854,.T.);
#16781=EDGE_CURVE('',#12589,#12593,#1734,.F.);
#16782=EDGE_CURVE('',#12595,#12590,#1735,.T.);
#16783=EDGE_CURVE('',#12594,#12595,#1736,.T.);
#16784=EDGE_CURVE('',#12596,#12597,#7855,.T.);
#16785=EDGE_CURVE('',#12598,#12596,#1737,.F.);
#16786=EDGE_CURVE('',#12593,#12598,#1738,.F.);
#16787=EDGE_CURVE('',#12599,#12594,#1739,.T.);
#16788=EDGE_CURVE('',#12597,#12599,#1740,.F.);
#16789=EDGE_CURVE('',#12600,#12601,#7856,.T.);
#16790=EDGE_CURVE('',#12596,#12600,#1741,.F.);
#16791=EDGE_CURVE('',#12601,#12597,#1742,.F.);
#16792=EDGE_CURVE('',#12602,#12603,#7857,.T.);
#16793=EDGE_CURVE('',#12604,#12602,#1743,.T.);
#16794=EDGE_CURVE('',#12600,#12604,#1744,.F.);
#16795=EDGE_CURVE('',#12605,#12601,#1745,.F.);
#16796=EDGE_CURVE('',#12603,#12605,#1746,.F.);
#16797=EDGE_CURVE('',#12606,#12607,#7858,.T.);
#16798=EDGE_CURVE('',#12608,#12606,#1747,.T.);
#16799=EDGE_CURVE('',#12602,#12608,#1748,.T.);
#16800=EDGE_CURVE('',#12607,#12603,#1749,.F.);
#16801=EDGE_CURVE('',#12609,#12610,#7859,.T.);
#16802=EDGE_CURVE('',#12611,#12609,#1750,.F.);
#16803=EDGE_CURVE('',#12606,#12611,#1751,.T.);
#16804=EDGE_CURVE('',#12612,#12607,#1752,.F.);
#16805=EDGE_CURVE('',#12610,#12612,#1753,.T.);
#16806=EDGE_CURVE('',#12613,#12614,#7860,.T.);
#16807=EDGE_CURVE('',#12609,#12613,#1754,.F.);
#16808=EDGE_CURVE('',#12615,#12610,#1755,.T.);
#16809=EDGE_CURVE('',#12614,#12615,#1756,.T.);
#16810=EDGE_CURVE('',#12616,#12617,#7861,.T.);
#16811=EDGE_CURVE('',#12618,#12616,#1757,.F.);
#16812=EDGE_CURVE('',#12613,#12618,#1758,.F.);
#16813=EDGE_CURVE('',#12619,#12614,#1759,.T.);
#16814=EDGE_CURVE('',#12617,#12619,#1760,.F.);
#16815=EDGE_CURVE('',#12620,#12621,#7862,.T.);
#16816=EDGE_CURVE('',#12616,#12620,#1761,.F.);
#16817=EDGE_CURVE('',#12621,#12617,#1762,.F.);
#16818=EDGE_CURVE('',#12622,#12623,#7863,.T.);
#16819=EDGE_CURVE('',#12624,#12622,#1763,.T.);
#16820=EDGE_CURVE('',#12620,#12624,#1764,.F.);
#16821=EDGE_CURVE('',#12625,#12621,#1765,.F.);
#16822=EDGE_CURVE('',#12623,#12625,#1766,.F.);
#16823=EDGE_CURVE('',#12626,#12627,#7864,.T.);
#16824=EDGE_CURVE('',#12628,#12626,#1767,.T.);
#16825=EDGE_CURVE('',#12622,#12628,#1768,.T.);
#16826=EDGE_CURVE('',#12627,#12623,#1769,.F.);
#16827=EDGE_CURVE('',#12629,#12630,#7865,.T.);
#16828=EDGE_CURVE('',#12631,#12629,#1770,.F.);
#16829=EDGE_CURVE('',#12626,#12631,#1771,.T.);
#16830=EDGE_CURVE('',#12632,#12627,#1772,.F.);
#16831=EDGE_CURVE('',#12630,#12632,#1773,.F.);
#16832=EDGE_CURVE('',#12633,#12634,#7866,.T.);
#16833=EDGE_CURVE('',#12629,#12633,#1774,.F.);
#16834=EDGE_CURVE('',#12634,#12630,#1775,.F.);
#16835=EDGE_CURVE('',#12635,#12636,#7867,.T.);
#16836=EDGE_CURVE('',#12637,#12635,#1776,.F.);
#16837=EDGE_CURVE('',#12633,#12637,#1777,.F.);
#16838=EDGE_CURVE('',#12638,#12634,#1778,.F.);
#16839=EDGE_CURVE('',#12636,#12638,#1779,.F.);
#16840=EDGE_CURVE('',#12639,#12640,#7868,.T.);
#16841=EDGE_CURVE('',#12635,#12639,#1780,.F.);
#16842=EDGE_CURVE('',#12640,#12636,#1781,.F.);
#16843=EDGE_CURVE('',#12641,#12642,#7869,.T.);
#16844=EDGE_CURVE('',#12643,#12641,#1782,.T.);
#16845=EDGE_CURVE('',#12639,#12643,#1783,.F.);
#16846=EDGE_CURVE('',#12644,#12640,#1784,.F.);
#16847=EDGE_CURVE('',#12642,#12644,#1785,.F.);
#16848=EDGE_CURVE('',#12645,#12646,#7870,.T.);
#16849=EDGE_CURVE('',#12647,#12645,#1786,.F.);
#16850=EDGE_CURVE('',#12641,#12647,#1787,.T.);
#16851=EDGE_CURVE('',#12646,#12642,#1788,.F.);
#16852=EDGE_CURVE('',#12648,#12649,#7871,.T.);
#16853=EDGE_CURVE('',#12645,#12648,#1789,.F.);
#16854=EDGE_CURVE('',#12650,#12646,#1790,.F.);
#16855=EDGE_CURVE('',#12649,#12650,#1791,.T.);
#16856=EDGE_CURVE('',#12651,#12652,#7872,.T.);
#16857=EDGE_CURVE('',#12653,#12651,#1792,.T.);
#16858=EDGE_CURVE('',#12648,#12653,#1793,.F.);
#16859=EDGE_CURVE('',#12654,#12649,#1794,.T.);
#16860=EDGE_CURVE('',#12652,#12654,#1795,.T.);
#16861=EDGE_CURVE('',#12655,#12656,#7873,.T.);
#16862=EDGE_CURVE('',#12657,#12655,#1796,.T.);
#16863=EDGE_CURVE('',#12658,#12657,#1797,.T.);
#16864=EDGE_CURVE('',#12658,#12659,#6219,.F.);
#16865=EDGE_CURVE('',#12660,#12659,#1798,.T.);
#16866=EDGE_CURVE('',#12656,#12660,#1799,.F.);
#16867=EDGE_CURVE('',#12661,#12662,#7874,.T.);
#16868=EDGE_CURVE('',#12663,#12661,#1800,.F.);
#16869=EDGE_CURVE('',#12655,#12663,#1801,.T.);
#16870=EDGE_CURVE('',#12662,#12656,#1802,.F.);
#16871=EDGE_CURVE('',#12664,#12665,#7875,.T.);
#16872=EDGE_CURVE('',#12661,#12664,#1803,.F.);
#16873=EDGE_CURVE('',#12666,#12662,#1804,.F.);
#16874=EDGE_CURVE('',#12665,#12666,#1805,.T.);
#16875=EDGE_CURVE('',#12667,#12668,#7876,.T.);
#16876=EDGE_CURVE('',#12669,#12667,#1806,.F.);
#16877=EDGE_CURVE('',#12664,#12669,#1807,.F.);
#16878=EDGE_CURVE('',#12670,#12665,#1808,.T.);
#16879=EDGE_CURVE('',#12668,#12670,#1809,.F.);
#16880=EDGE_CURVE('',#12671,#12672,#7877,.T.);
#16881=EDGE_CURVE('',#12667,#12671,#1810,.F.);
#16882=EDGE_CURVE('',#12672,#12668,#1811,.F.);
#16883=EDGE_CURVE('',#12673,#12674,#7878,.T.);
#16884=EDGE_CURVE('',#12675,#12673,#1812,.F.);
#16885=EDGE_CURVE('',#12671,#12675,#1813,.F.);
#16886=EDGE_CURVE('',#12676,#12672,#1814,.F.);
#16887=EDGE_CURVE('',#12674,#12676,#1815,.F.);
#16888=EDGE_CURVE('',#12677,#12678,#7879,.T.);
#16889=EDGE_CURVE('',#12673,#12677,#1816,.F.);
#16890=EDGE_CURVE('',#12678,#12674,#1817,.F.);
#16891=EDGE_CURVE('',#12679,#12680,#7880,.T.);
#16892=EDGE_CURVE('',#12681,#12679,#1818,.F.);
#16893=EDGE_CURVE('',#12677,#12681,#1819,.F.);
#16894=EDGE_CURVE('',#12682,#12678,#1820,.F.);
#16895=EDGE_CURVE('',#12680,#12682,#1821,.T.);
#16896=EDGE_CURVE('',#12683,#12684,#7881,.T.);
#16897=EDGE_CURVE('',#12679,#12683,#1822,.F.);
#16898=EDGE_CURVE('',#12685,#12680,#1823,.T.);
#16899=EDGE_CURVE('',#12684,#12685,#1824,.T.);
#16900=EDGE_CURVE('',#12686,#12687,#7882,.T.);
#16901=EDGE_CURVE('',#12688,#12686,#1825,.F.);
#16902=EDGE_CURVE('',#12683,#12688,#1826,.F.);
#16903=EDGE_CURVE('',#12689,#12684,#1827,.T.);
#16904=EDGE_CURVE('',#12687,#12689,#1828,.F.);
#16905=EDGE_CURVE('',#12690,#12691,#7883,.T.);
#16906=EDGE_CURVE('',#12686,#12690,#1829,.F.);
#16907=EDGE_CURVE('',#12691,#12687,#1830,.F.);
#16908=EDGE_CURVE('',#12692,#12693,#7884,.T.);
#16909=EDGE_CURVE('',#12694,#12692,#1831,.T.);
#16910=EDGE_CURVE('',#12690,#12694,#1832,.F.);
#16911=EDGE_CURVE('',#12695,#12691,#1833,.F.);
#16912=EDGE_CURVE('',#12693,#12695,#1834,.F.);
#16913=EDGE_CURVE('',#12696,#12697,#7885,.T.);
#16914=EDGE_CURVE('',#12698,#12696,#1835,.T.);
#16915=EDGE_CURVE('',#12692,#12698,#1836,.T.);
#16916=EDGE_CURVE('',#12697,#12693,#1837,.F.);
#16917=EDGE_CURVE('',#12699,#12700,#7886,.T.);
#16918=EDGE_CURVE('',#12701,#12699,#1838,.F.);
#16919=EDGE_CURVE('',#12696,#12701,#1839,.T.);
#16920=EDGE_CURVE('',#12702,#12697,#1840,.F.);
#16921=EDGE_CURVE('',#12700,#12702,#1841,.T.);
#16922=EDGE_CURVE('',#12703,#12704,#7887,.T.);
#16923=EDGE_CURVE('',#12699,#12703,#1842,.F.);
#16924=EDGE_CURVE('',#12705,#12700,#1843,.T.);
#16925=EDGE_CURVE('',#12704,#12705,#1844,.T.);
#16926=EDGE_CURVE('',#12706,#12707,#7888,.T.);
#16927=EDGE_CURVE('',#12708,#12706,#1845,.F.);
#16928=EDGE_CURVE('',#12703,#12708,#1846,.F.);
#16929=EDGE_CURVE('',#12709,#12704,#1847,.T.);
#16930=EDGE_CURVE('',#12707,#12709,#1848,.F.);
#16931=EDGE_CURVE('',#12710,#12711,#7889,.T.);
#16932=EDGE_CURVE('',#12706,#12710,#1849,.F.);
#16933=EDGE_CURVE('',#12711,#12707,#1850,.F.);
#16934=EDGE_CURVE('',#12712,#12713,#7890,.T.);
#16935=EDGE_CURVE('',#12714,#12712,#1851,.T.);
#16936=EDGE_CURVE('',#12710,#12714,#1852,.F.);
#16937=EDGE_CURVE('',#12715,#12711,#1853,.F.);
#16938=EDGE_CURVE('',#12713,#12715,#1854,.F.);
#16939=EDGE_CURVE('',#12716,#12717,#7891,.T.);
#16940=EDGE_CURVE('',#12718,#12716,#1855,.T.);
#16941=EDGE_CURVE('',#12712,#12718,#1856,.T.);
#16942=EDGE_CURVE('',#12717,#12713,#1857,.F.);
#16943=EDGE_CURVE('',#12719,#12720,#7892,.T.);
#16944=EDGE_CURVE('',#12721,#12719,#1858,.F.);
#16945=EDGE_CURVE('',#12716,#12721,#1859,.T.);
#16946=EDGE_CURVE('',#12722,#12717,#1860,.F.);
#16947=EDGE_CURVE('',#12720,#12722,#1861,.F.);
#16948=EDGE_CURVE('',#12723,#12724,#7893,.T.);
#16949=EDGE_CURVE('',#12719,#12723,#1862,.F.);
#16950=EDGE_CURVE('',#12724,#12720,#1863,.F.);
#16951=EDGE_CURVE('',#12725,#12726,#7894,.T.);
#16952=EDGE_CURVE('',#12727,#12725,#1864,.F.);
#16953=EDGE_CURVE('',#12723,#12727,#1865,.F.);
#16954=EDGE_CURVE('',#12728,#12724,#1866,.F.);
#16955=EDGE_CURVE('',#12726,#12728,#1867,.F.);
#16956=EDGE_CURVE('',#12729,#12730,#7895,.T.);
#16957=EDGE_CURVE('',#12725,#12729,#1868,.F.);
#16958=EDGE_CURVE('',#12730,#12726,#1869,.F.);
#16959=EDGE_CURVE('',#12731,#12732,#7896,.T.);
#16960=EDGE_CURVE('',#12733,#12731,#1870,.T.);
#16961=EDGE_CURVE('',#12729,#12733,#1871,.F.);
#16962=EDGE_CURVE('',#12734,#12730,#1872,.F.);
#16963=EDGE_CURVE('',#12732,#12734,#1873,.F.);
#16964=EDGE_CURVE('',#12735,#12736,#7897,.T.);
#16965=EDGE_CURVE('',#12737,#12735,#1874,.F.);
#16966=EDGE_CURVE('',#12731,#12737,#1875,.T.);
#16967=EDGE_CURVE('',#12736,#12732,#1876,.F.);
#16968=EDGE_CURVE('',#12738,#12739,#7898,.T.);
#16969=EDGE_CURVE('',#12735,#12738,#1877,.F.);
#16970=EDGE_CURVE('',#12740,#12736,#1878,.F.);
#16971=EDGE_CURVE('',#12739,#12740,#1879,.T.);
#16972=EDGE_CURVE('',#12741,#12742,#7899,.T.);
#16973=EDGE_CURVE('',#12743,#12741,#1880,.T.);
#16974=EDGE_CURVE('',#12738,#12743,#1881,.F.);
#16975=EDGE_CURVE('',#12744,#12739,#1882,.T.);
#16976=EDGE_CURVE('',#12742,#12744,#1883,.T.);
#16977=EDGE_CURVE('',#12745,#12746,#7900,.T.);
#16978=EDGE_CURVE('',#12747,#12745,#1884,.T.);
#16979=EDGE_CURVE('',#12748,#12747,#1885,.T.);
#16980=EDGE_CURVE('',#12748,#12749,#6220,.F.);
#16981=EDGE_CURVE('',#12750,#12749,#1886,.T.);
#16982=EDGE_CURVE('',#12746,#12750,#1887,.F.);
#16983=EDGE_CURVE('',#12751,#12752,#7901,.T.);
#16984=EDGE_CURVE('',#12753,#12751,#1888,.F.);
#16985=EDGE_CURVE('',#12745,#12753,#1889,.T.);
#16986=EDGE_CURVE('',#12752,#12746,#1890,.F.);
#16987=EDGE_CURVE('',#12754,#12755,#7902,.T.);
#16988=EDGE_CURVE('',#12751,#12754,#1891,.F.);
#16989=EDGE_CURVE('',#12756,#12752,#1892,.F.);
#16990=EDGE_CURVE('',#12755,#12756,#1893,.T.);
#16991=EDGE_CURVE('',#12757,#12758,#7903,.T.);
#16992=EDGE_CURVE('',#12759,#12757,#1894,.F.);
#16993=EDGE_CURVE('',#12754,#12759,#1895,.F.);
#16994=EDGE_CURVE('',#12760,#12755,#1896,.T.);
#16995=EDGE_CURVE('',#12758,#12760,#1897,.F.);
#16996=EDGE_CURVE('',#12761,#12762,#7904,.T.);
#16997=EDGE_CURVE('',#12757,#12761,#1898,.F.);
#16998=EDGE_CURVE('',#12762,#12758,#1899,.F.);
#16999=EDGE_CURVE('',#12763,#12764,#7905,.T.);
#17000=EDGE_CURVE('',#12765,#12763,#1900,.F.);
#17001=EDGE_CURVE('',#12761,#12765,#1901,.F.);
#17002=EDGE_CURVE('',#12766,#12762,#1902,.F.);
#17003=EDGE_CURVE('',#12764,#12766,#1903,.F.);
#17004=EDGE_CURVE('',#12767,#12768,#7906,.T.);
#17005=EDGE_CURVE('',#12763,#12767,#1904,.F.);
#17006=EDGE_CURVE('',#12768,#12764,#1905,.F.);
#17007=EDGE_CURVE('',#12769,#12770,#7907,.T.);
#17008=EDGE_CURVE('',#12771,#12769,#1906,.F.);
#17009=EDGE_CURVE('',#12767,#12771,#1907,.F.);
#17010=EDGE_CURVE('',#12772,#12768,#1908,.F.);
#17011=EDGE_CURVE('',#12770,#12772,#1909,.T.);
#17012=EDGE_CURVE('',#12773,#12774,#7908,.T.);
#17013=EDGE_CURVE('',#12769,#12773,#1910,.F.);
#17014=EDGE_CURVE('',#12775,#12770,#1911,.T.);
#17015=EDGE_CURVE('',#12774,#12775,#1912,.T.);
#17016=EDGE_CURVE('',#12776,#12777,#7909,.T.);
#17017=EDGE_CURVE('',#12778,#12776,#1913,.F.);
#17018=EDGE_CURVE('',#12773,#12778,#1914,.F.);
#17019=EDGE_CURVE('',#12779,#12774,#1915,.T.);
#17020=EDGE_CURVE('',#12777,#12779,#1916,.F.);
#17021=EDGE_CURVE('',#12780,#12781,#7910,.T.);
#17022=EDGE_CURVE('',#12776,#12780,#1917,.F.);
#17023=EDGE_CURVE('',#12781,#12777,#1918,.F.);
#17024=EDGE_CURVE('',#12782,#12783,#7911,.T.);
#17025=EDGE_CURVE('',#12784,#12782,#1919,.T.);
#17026=EDGE_CURVE('',#12780,#12784,#1920,.F.);
#17027=EDGE_CURVE('',#12785,#12781,#1921,.F.);
#17028=EDGE_CURVE('',#12783,#12785,#1922,.F.);
#17029=EDGE_CURVE('',#12786,#12787,#7912,.T.);
#17030=EDGE_CURVE('',#12788,#12786,#1923,.T.);
#17031=EDGE_CURVE('',#12782,#12788,#1924,.T.);
#17032=EDGE_CURVE('',#12787,#12783,#1925,.F.);
#17033=EDGE_CURVE('',#12789,#12790,#7913,.T.);
#17034=EDGE_CURVE('',#12791,#12789,#1926,.F.);
#17035=EDGE_CURVE('',#12786,#12791,#1927,.T.);
#17036=EDGE_CURVE('',#12792,#12787,#1928,.F.);
#17037=EDGE_CURVE('',#12790,#12792,#1929,.T.);
#17038=EDGE_CURVE('',#12793,#12794,#7914,.T.);
#17039=EDGE_CURVE('',#12789,#12793,#1930,.F.);
#17040=EDGE_CURVE('',#12795,#12790,#1931,.T.);
#17041=EDGE_CURVE('',#12794,#12795,#1932,.T.);
#17042=EDGE_CURVE('',#12796,#12797,#7915,.T.);
#17043=EDGE_CURVE('',#12798,#12796,#1933,.F.);
#17044=EDGE_CURVE('',#12793,#12798,#1934,.F.);
#17045=EDGE_CURVE('',#12799,#12794,#1935,.T.);
#17046=EDGE_CURVE('',#12797,#12799,#1936,.F.);
#17047=EDGE_CURVE('',#12800,#12801,#7916,.T.);
#17048=EDGE_CURVE('',#12796,#12800,#1937,.F.);
#17049=EDGE_CURVE('',#12801,#12797,#1938,.F.);
#17050=EDGE_CURVE('',#12802,#12803,#7917,.T.);
#17051=EDGE_CURVE('',#12804,#12802,#1939,.T.);
#17052=EDGE_CURVE('',#12800,#12804,#1940,.F.);
#17053=EDGE_CURVE('',#12805,#12801,#1941,.F.);
#17054=EDGE_CURVE('',#12803,#12805,#1942,.F.);
#17055=EDGE_CURVE('',#12806,#12807,#7918,.T.);
#17056=EDGE_CURVE('',#12808,#12806,#1943,.T.);
#17057=EDGE_CURVE('',#12802,#12808,#1944,.T.);
#17058=EDGE_CURVE('',#12807,#12803,#1945,.F.);
#17059=EDGE_CURVE('',#12809,#12810,#7919,.T.);
#17060=EDGE_CURVE('',#12811,#12809,#1946,.F.);
#17061=EDGE_CURVE('',#12806,#12811,#1947,.T.);
#17062=EDGE_CURVE('',#12812,#12807,#1948,.F.);
#17063=EDGE_CURVE('',#12810,#12812,#1949,.F.);
#17064=EDGE_CURVE('',#12813,#12814,#7920,.T.);
#17065=EDGE_CURVE('',#12809,#12813,#1950,.F.);
#17066=EDGE_CURVE('',#12814,#12810,#1951,.F.);
#17067=EDGE_CURVE('',#12815,#12816,#7921,.T.);
#17068=EDGE_CURVE('',#12817,#12815,#1952,.F.);
#17069=EDGE_CURVE('',#12813,#12817,#1953,.F.);
#17070=EDGE_CURVE('',#12818,#12814,#1954,.F.);
#17071=EDGE_CURVE('',#12816,#12818,#1955,.F.);
#17072=EDGE_CURVE('',#12819,#12820,#7922,.T.);
#17073=EDGE_CURVE('',#12815,#12819,#1956,.F.);
#17074=EDGE_CURVE('',#12820,#12816,#1957,.F.);
#17075=EDGE_CURVE('',#12821,#12822,#7923,.T.);
#17076=EDGE_CURVE('',#12823,#12821,#1958,.T.);
#17077=EDGE_CURVE('',#12819,#12823,#1959,.F.);
#17078=EDGE_CURVE('',#12824,#12820,#1960,.F.);
#17079=EDGE_CURVE('',#12822,#12824,#1961,.F.);
#17080=EDGE_CURVE('',#12825,#12826,#7924,.T.);
#17081=EDGE_CURVE('',#12827,#12825,#1962,.F.);
#17082=EDGE_CURVE('',#12821,#12827,#1963,.T.);
#17083=EDGE_CURVE('',#12826,#12822,#1964,.F.);
#17084=EDGE_CURVE('',#12828,#12829,#7925,.T.);
#17085=EDGE_CURVE('',#12825,#12828,#1965,.F.);
#17086=EDGE_CURVE('',#12830,#12826,#1966,.F.);
#17087=EDGE_CURVE('',#12829,#12830,#1967,.T.);
#17088=EDGE_CURVE('',#12831,#12832,#7926,.T.);
#17089=EDGE_CURVE('',#12833,#12831,#1968,.T.);
#17090=EDGE_CURVE('',#12828,#12833,#1969,.F.);
#17091=EDGE_CURVE('',#12834,#12829,#1970,.T.);
#17092=EDGE_CURVE('',#12832,#12834,#1971,.T.);
#17093=EDGE_CURVE('',#12835,#12836,#7927,.T.);
#17094=EDGE_CURVE('',#12837,#12835,#1972,.T.);
#17095=EDGE_CURVE('',#12838,#12837,#1973,.T.);
#17096=EDGE_CURVE('',#12838,#12839,#6221,.F.);
#17097=EDGE_CURVE('',#12840,#12839,#1974,.T.);
#17098=EDGE_CURVE('',#12836,#12840,#1975,.F.);
#17099=EDGE_CURVE('',#12841,#12842,#7928,.T.);
#17100=EDGE_CURVE('',#12843,#12841,#1976,.F.);
#17101=EDGE_CURVE('',#12835,#12843,#1977,.T.);
#17102=EDGE_CURVE('',#12842,#12836,#1978,.F.);
#17103=EDGE_CURVE('',#12844,#12845,#7929,.T.);
#17104=EDGE_CURVE('',#12841,#12844,#1979,.F.);
#17105=EDGE_CURVE('',#12846,#12842,#1980,.F.);
#17106=EDGE_CURVE('',#12845,#12846,#1981,.T.);
#17107=EDGE_CURVE('',#12847,#12848,#7930,.T.);
#17108=EDGE_CURVE('',#12849,#12847,#1982,.F.);
#17109=EDGE_CURVE('',#12844,#12849,#1983,.F.);
#17110=EDGE_CURVE('',#12850,#12845,#1984,.T.);
#17111=EDGE_CURVE('',#12848,#12850,#1985,.F.);
#17112=EDGE_CURVE('',#12851,#12852,#7931,.T.);
#17113=EDGE_CURVE('',#12847,#12851,#1986,.F.);
#17114=EDGE_CURVE('',#12852,#12848,#1987,.F.);
#17115=EDGE_CURVE('',#12853,#12854,#7932,.T.);
#17116=EDGE_CURVE('',#12855,#12853,#1988,.F.);
#17117=EDGE_CURVE('',#12851,#12855,#1989,.F.);
#17118=EDGE_CURVE('',#12856,#12852,#1990,.F.);
#17119=EDGE_CURVE('',#12854,#12856,#1991,.F.);
#17120=EDGE_CURVE('',#12857,#12858,#7933,.T.);
#17121=EDGE_CURVE('',#12853,#12857,#1992,.F.);
#17122=EDGE_CURVE('',#12858,#12854,#1993,.F.);
#17123=EDGE_CURVE('',#12859,#12860,#7934,.T.);
#17124=EDGE_CURVE('',#12861,#12859,#1994,.F.);
#17125=EDGE_CURVE('',#12857,#12861,#1995,.F.);
#17126=EDGE_CURVE('',#12862,#12858,#1996,.F.);
#17127=EDGE_CURVE('',#12860,#12862,#1997,.T.);
#17128=EDGE_CURVE('',#12863,#12864,#7935,.T.);
#17129=EDGE_CURVE('',#12859,#12863,#1998,.F.);
#17130=EDGE_CURVE('',#12865,#12860,#1999,.T.);
#17131=EDGE_CURVE('',#12864,#12865,#2000,.T.);
#17132=EDGE_CURVE('',#12866,#12867,#7936,.T.);
#17133=EDGE_CURVE('',#12868,#12866,#2001,.F.);
#17134=EDGE_CURVE('',#12863,#12868,#2002,.F.);
#17135=EDGE_CURVE('',#12869,#12864,#2003,.T.);
#17136=EDGE_CURVE('',#12867,#12869,#2004,.F.);
#17137=EDGE_CURVE('',#12870,#12871,#7937,.T.);
#17138=EDGE_CURVE('',#12866,#12870,#2005,.F.);
#17139=EDGE_CURVE('',#12871,#12867,#2006,.F.);
#17140=EDGE_CURVE('',#12872,#12873,#7938,.T.);
#17141=EDGE_CURVE('',#12874,#12872,#2007,.T.);
#17142=EDGE_CURVE('',#12870,#12874,#2008,.F.);
#17143=EDGE_CURVE('',#12875,#12871,#2009,.F.);
#17144=EDGE_CURVE('',#12873,#12875,#2010,.F.);
#17145=EDGE_CURVE('',#12876,#12877,#7939,.T.);
#17146=EDGE_CURVE('',#12878,#12876,#2011,.T.);
#17147=EDGE_CURVE('',#12872,#12878,#2012,.T.);
#17148=EDGE_CURVE('',#12877,#12873,#2013,.F.);
#17149=EDGE_CURVE('',#12879,#12880,#7940,.T.);
#17150=EDGE_CURVE('',#12881,#12879,#2014,.F.);
#17151=EDGE_CURVE('',#12876,#12881,#2015,.T.);
#17152=EDGE_CURVE('',#12882,#12877,#2016,.F.);
#17153=EDGE_CURVE('',#12880,#12882,#2017,.T.);
#17154=EDGE_CURVE('',#12883,#12884,#7941,.T.);
#17155=EDGE_CURVE('',#12879,#12883,#2018,.F.);
#17156=EDGE_CURVE('',#12885,#12880,#2019,.T.);
#17157=EDGE_CURVE('',#12884,#12885,#2020,.T.);
#17158=EDGE_CURVE('',#12886,#12887,#7942,.T.);
#17159=EDGE_CURVE('',#12888,#12886,#2021,.F.);
#17160=EDGE_CURVE('',#12883,#12888,#2022,.F.);
#17161=EDGE_CURVE('',#12889,#12884,#2023,.T.);
#17162=EDGE_CURVE('',#12887,#12889,#2024,.F.);
#17163=EDGE_CURVE('',#12890,#12891,#7943,.T.);
#17164=EDGE_CURVE('',#12886,#12890,#2025,.F.);
#17165=EDGE_CURVE('',#12891,#12887,#2026,.F.);
#17166=EDGE_CURVE('',#12892,#12893,#7944,.T.);
#17167=EDGE_CURVE('',#12894,#12892,#2027,.T.);
#17168=EDGE_CURVE('',#12890,#12894,#2028,.F.);
#17169=EDGE_CURVE('',#12895,#12891,#2029,.F.);
#17170=EDGE_CURVE('',#12893,#12895,#2030,.F.);
#17171=EDGE_CURVE('',#12896,#12897,#7945,.T.);
#17172=EDGE_CURVE('',#12898,#12896,#2031,.T.);
#17173=EDGE_CURVE('',#12892,#12898,#2032,.T.);
#17174=EDGE_CURVE('',#12897,#12893,#2033,.F.);
#17175=EDGE_CURVE('',#12899,#12900,#7946,.T.);
#17176=EDGE_CURVE('',#12901,#12899,#2034,.F.);
#17177=EDGE_CURVE('',#12896,#12901,#2035,.T.);
#17178=EDGE_CURVE('',#12902,#12897,#2036,.F.);
#17179=EDGE_CURVE('',#12900,#12902,#2037,.F.);
#17180=EDGE_CURVE('',#12903,#12904,#7947,.T.);
#17181=EDGE_CURVE('',#12899,#12903,#2038,.F.);
#17182=EDGE_CURVE('',#12904,#12900,#2039,.F.);
#17183=EDGE_CURVE('',#12905,#12906,#7948,.T.);
#17184=EDGE_CURVE('',#12907,#12905,#2040,.F.);
#17185=EDGE_CURVE('',#12903,#12907,#2041,.F.);
#17186=EDGE_CURVE('',#12908,#12904,#2042,.F.);
#17187=EDGE_CURVE('',#12906,#12908,#2043,.F.);
#17188=EDGE_CURVE('',#12909,#12910,#7949,.T.);
#17189=EDGE_CURVE('',#12905,#12909,#2044,.F.);
#17190=EDGE_CURVE('',#12910,#12906,#2045,.F.);
#17191=EDGE_CURVE('',#12911,#12912,#7950,.T.);
#17192=EDGE_CURVE('',#12913,#12911,#2046,.T.);
#17193=EDGE_CURVE('',#12909,#12913,#2047,.F.);
#17194=EDGE_CURVE('',#12914,#12910,#2048,.F.);
#17195=EDGE_CURVE('',#12912,#12914,#2049,.F.);
#17196=EDGE_CURVE('',#12915,#12916,#7951,.T.);
#17197=EDGE_CURVE('',#12917,#12915,#2050,.F.);
#17198=EDGE_CURVE('',#12911,#12917,#2051,.T.);
#17199=EDGE_CURVE('',#12916,#12912,#2052,.F.);
#17200=EDGE_CURVE('',#12918,#12919,#7952,.T.);
#17201=EDGE_CURVE('',#12915,#12918,#2053,.F.);
#17202=EDGE_CURVE('',#12920,#12916,#2054,.F.);
#17203=EDGE_CURVE('',#12919,#12920,#2055,.T.);
#17204=EDGE_CURVE('',#12921,#12922,#7953,.T.);
#17205=EDGE_CURVE('',#12923,#12921,#2056,.T.);
#17206=EDGE_CURVE('',#12918,#12923,#2057,.F.);
#17207=EDGE_CURVE('',#12924,#12919,#2058,.T.);
#17208=EDGE_CURVE('',#12922,#12924,#2059,.T.);
#17209=EDGE_CURVE('',#12925,#12922,#2060,.T.);
#17210=EDGE_CURVE('',#12925,#12926,#6222,.T.);
#17211=EDGE_CURVE('',#12921,#12926,#2061,.T.);
#17212=EDGE_CURVE('',#12927,#12832,#2062,.T.);
#17213=EDGE_CURVE('',#12927,#12928,#6223,.T.);
#17214=EDGE_CURVE('',#12831,#12928,#2063,.T.);
#17215=EDGE_CURVE('',#12929,#12742,#2064,.T.);
#17216=EDGE_CURVE('',#12929,#12930,#6224,.T.);
#17217=EDGE_CURVE('',#12741,#12930,#2065,.T.);
#17218=EDGE_CURVE('',#12931,#12652,#2066,.T.);
#17219=EDGE_CURVE('',#12931,#12932,#6225,.T.);
#17220=EDGE_CURVE('',#12651,#12932,#2067,.T.);
#17221=EDGE_CURVE('',#12933,#12563,#2068,.T.);
#17222=EDGE_CURVE('',#12562,#12933,#6226,.T.);
#17223=EDGE_CURVE('',#12934,#12553,#2069,.T.);
#17224=EDGE_CURVE('',#12935,#12934,#6227,.F.);
#17225=EDGE_CURVE('',#12552,#12935,#2070,.F.);
#17226=EDGE_CURVE('',#12541,#12936,#2071,.T.);
#17227=EDGE_CURVE('',#12936,#12937,#2072,.T.);
#17228=EDGE_CURVE('',#12937,#12938,#6228,.T.);
#17229=EDGE_CURVE('',#12939,#12938,#2073,.T.);
#17230=EDGE_CURVE('',#12540,#12939,#2074,.T.);
#17231=EDGE_CURVE('',#12431,#12940,#2075,.T.);
#17232=EDGE_CURVE('',#12940,#12941,#2076,.T.);
#17233=EDGE_CURVE('',#12941,#12942,#6229,.T.);
#17234=EDGE_CURVE('',#12943,#12942,#2077,.T.);
#17235=EDGE_CURVE('',#12430,#12943,#2078,.T.);
#17236=EDGE_CURVE('',#12321,#12944,#2079,.T.);
#17237=EDGE_CURVE('',#12944,#12945,#2080,.T.);
#17238=EDGE_CURVE('',#12945,#12946,#6230,.T.);
#17239=EDGE_CURVE('',#12947,#12946,#2081,.T.);
#17240=EDGE_CURVE('',#12320,#12947,#2082,.T.);
#17241=EDGE_CURVE('',#12211,#12948,#2083,.T.);
#17242=EDGE_CURVE('',#12948,#12949,#2084,.T.);
#17243=EDGE_CURVE('',#12949,#12950,#6231,.T.);
#17244=EDGE_CURVE('',#12951,#12950,#2085,.T.);
#17245=EDGE_CURVE('',#12210,#12951,#2086,.T.);
#17246=EDGE_CURVE('',#12101,#12952,#2087,.T.);
#17247=EDGE_CURVE('',#12952,#12953,#2088,.T.);
#17248=EDGE_CURVE('',#12953,#12954,#6232,.T.);
#17249=EDGE_CURVE('',#12955,#12954,#2089,.T.);
#17250=EDGE_CURVE('',#12100,#12955,#2090,.T.);
#17251=EDGE_CURVE('',#12085,#12956,#2091,.T.);
#17252=EDGE_CURVE('',#12956,#12957,#2092,.T.);
#17253=EDGE_CURVE('',#12957,#12958,#6233,.T.);
#17254=EDGE_CURVE('',#12959,#12958,#2093,.T.);
#17255=EDGE_CURVE('',#12084,#12959,#2094,.T.);
#17256=EDGE_CURVE('',#12960,#12960,#6234,.T.);
#17257=EDGE_CURVE('',#12960,#12961,#7954,.T.);
#17258=EDGE_CURVE('',#12961,#12961,#6235,.T.);
#17259=EDGE_CURVE('',#12962,#12963,#6236,.T.);
#17260=EDGE_CURVE('',#12963,#12964,#7955,.T.);
#17261=EDGE_CURVE('',#12965,#12964,#6237,.T.);
#17262=EDGE_CURVE('',#12965,#12962,#7956,.T.);
#17263=EDGE_CURVE('',#12964,#12966,#7957,.T.);
#17264=EDGE_CURVE('',#12966,#12967,#6238,.T.);
#17265=EDGE_CURVE('',#12967,#12968,#7958,.T.);
#17266=EDGE_CURVE('',#12968,#12965,#7959,.T.);
#17267=EDGE_CURVE('',#12969,#12969,#6239,.T.);
#17268=EDGE_CURVE('',#12969,#12970,#7960,.T.);
#17269=EDGE_CURVE('',#12970,#12970,#6240,.T.);
#17270=EDGE_CURVE('',#12971,#12972,#6241,.T.);
#17271=EDGE_CURVE('',#12972,#12973,#7961,.T.);
#17272=EDGE_CURVE('',#12974,#12973,#6242,.T.);
#17273=EDGE_CURVE('',#12974,#12971,#7962,.T.);
#17274=EDGE_CURVE('',#12975,#12976,#7963,.T.);
#17275=EDGE_CURVE('',#12976,#12977,#6243,.T.);
#17276=EDGE_CURVE('',#12977,#12974,#7964,.T.);
#17277=EDGE_CURVE('',#12973,#12975,#7965,.T.);
#17278=EDGE_CURVE('',#12978,#12978,#6244,.T.);
#17279=EDGE_CURVE('',#12978,#12979,#7966,.T.);
#17280=EDGE_CURVE('',#12979,#12979,#6245,.T.);
#17281=EDGE_CURVE('',#12980,#12967,#7967,.T.);
#17282=EDGE_CURVE('',#12981,#12980,#7968,.T.);
#17283=EDGE_CURVE('',#12981,#12968,#7969,.T.);
#17284=EDGE_CURVE('',#12982,#12977,#7970,.T.);
#17285=EDGE_CURVE('',#12982,#12983,#7971,.T.);
#17286=EDGE_CURVE('',#12983,#12984,#7972,.T.);
#17287=EDGE_CURVE('',#12984,#12971,#7973,.T.);
#17288=EDGE_CURVE('',#12981,#12985,#7974,.T.);
#17289=EDGE_CURVE('',#12985,#12975,#7975,.T.);
#17290=EDGE_CURVE('',#12972,#12962,#7976,.T.);
#17291=EDGE_CURVE('',#12986,#12984,#6246,.T.);
#17292=EDGE_CURVE('',#12987,#12986,#7977,.T.);
#17293=EDGE_CURVE('',#12988,#12987,#6247,.T.);
#17294=EDGE_CURVE('',#12989,#12988,#7978,.T.);
#17295=EDGE_CURVE('',#12990,#12989,#6248,.T.);
#17296=EDGE_CURVE('',#12991,#12990,#7979,.T.);
#17297=EDGE_CURVE('',#12992,#12991,#6249,.T.);
#17298=EDGE_CURVE('',#12993,#12992,#7980,.T.);
#17299=EDGE_CURVE('',#12994,#12993,#7981,.T.);
#17300=EDGE_CURVE('',#12995,#12994,#7982,.T.);
#17301=EDGE_CURVE('',#12996,#12995,#7983,.T.);
#17302=EDGE_CURVE('',#12997,#12996,#7984,.T.);
#17303=EDGE_CURVE('',#12998,#12997,#6250,.T.);
#17304=EDGE_CURVE('',#12999,#12998,#7985,.T.);
#17305=EDGE_CURVE('',#13000,#12999,#6251,.T.);
#17306=EDGE_CURVE('',#13001,#13000,#7986,.T.);
#17307=EDGE_CURVE('',#13002,#13001,#7987,.T.);
#17308=EDGE_CURVE('',#13003,#13002,#7988,.T.);
#17309=EDGE_CURVE('',#13004,#13003,#7989,.T.);
#17310=EDGE_CURVE('',#13005,#13004,#7990,.T.);
#17311=EDGE_CURVE('',#13006,#13005,#6252,.T.);
#17312=EDGE_CURVE('',#13007,#13006,#7991,.T.);
#17313=EDGE_CURVE('',#13008,#13007,#6253,.T.);
#17314=EDGE_CURVE('',#13009,#13008,#7992,.T.);
#17315=EDGE_CURVE('',#13010,#13009,#6254,.T.);
#17316=EDGE_CURVE('',#13011,#13010,#7993,.T.);
#17317=EDGE_CURVE('',#13012,#13011,#6255,.T.);
#17318=EDGE_CURVE('',#12963,#13012,#7994,.T.);
#17319=EDGE_CURVE('',#13013,#13013,#6256,.T.);
#17320=EDGE_CURVE('',#13014,#13014,#6257,.T.);
#17321=EDGE_CURVE('',#12926,#12949,#2095,.T.);
#17322=EDGE_CURVE('',#12950,#12925,#2096,.T.);
#17323=EDGE_CURVE('',#12928,#12945,#2097,.T.);
#17324=EDGE_CURVE('',#12946,#12927,#2098,.T.);
#17325=EDGE_CURVE('',#12930,#12941,#2099,.T.);
#17326=EDGE_CURVE('',#12942,#12929,#2100,.T.);
#17327=EDGE_CURVE('',#12932,#12937,#2101,.T.);
#17328=EDGE_CURVE('',#12938,#12931,#2102,.T.);
#17329=EDGE_CURVE('',#12958,#12933,#2103,.T.);
#17330=EDGE_CURVE('',#12557,#12074,#2104,.T.);
#17331=EDGE_CURVE('',#12564,#12957,#2105,.T.);
#17332=EDGE_CURVE('',#12075,#12556,#2106,.T.);
#17333=EDGE_CURVE('',#12954,#12546,#2107,.T.);
#17334=EDGE_CURVE('',#12935,#12090,#2108,.T.);
#17335=EDGE_CURVE('',#12549,#12953,#2109,.T.);
#17336=EDGE_CURVE('',#12091,#12934,#2110,.T.);
#17337=EDGE_CURVE('',#12839,#12107,#2111,.T.);
#17338=EDGE_CURVE('',#12108,#12838,#2112,.T.);
#17339=EDGE_CURVE('',#12749,#12217,#2113,.T.);
#17340=EDGE_CURVE('',#12218,#12748,#2114,.T.);
#17341=EDGE_CURVE('',#12659,#12327,#2115,.T.);
#17342=EDGE_CURVE('',#12328,#12658,#2116,.T.);
#17343=EDGE_CURVE('',#12569,#12437,#2117,.T.);
#17344=EDGE_CURVE('',#12438,#12568,#2118,.T.);
#17345=EDGE_CURVE('',#13015,#13016,#7995,.T.);
#17346=EDGE_CURVE('',#13016,#13017,#7996,.T.);
#17347=EDGE_CURVE('',#13017,#13018,#7997,.T.);
#17348=EDGE_CURVE('',#13015,#13018,#7998,.T.);
#17349=EDGE_CURVE('',#13016,#13019,#7999,.T.);
#17350=EDGE_CURVE('',#13019,#13020,#8000,.T.);
#17351=EDGE_CURVE('',#13020,#13017,#8001,.T.);
#17352=EDGE_CURVE('',#13019,#13021,#8002,.T.);
#17353=EDGE_CURVE('',#13021,#13022,#8003,.T.);
#17354=EDGE_CURVE('',#13022,#13020,#8004,.T.);
#17355=EDGE_CURVE('',#13021,#13023,#8005,.T.);
#17356=EDGE_CURVE('',#13023,#13024,#8006,.T.);
#17357=EDGE_CURVE('',#13024,#13022,#8007,.T.);
#17358=EDGE_CURVE('',#13023,#13025,#8008,.T.);
#17359=EDGE_CURVE('',#13025,#13026,#8009,.T.);
#17360=EDGE_CURVE('',#13026,#13024,#8010,.T.);
#17361=EDGE_CURVE('',#13025,#13027,#8011,.T.);
#17362=EDGE_CURVE('',#13027,#13028,#8012,.T.);
#17363=EDGE_CURVE('',#13028,#13026,#8013,.T.);
#17364=EDGE_CURVE('',#13027,#13015,#8014,.T.);
#17365=EDGE_CURVE('',#13018,#13028,#8015,.T.);
#17366=EDGE_CURVE('',#13029,#13029,#6258,.T.);
#17367=EDGE_CURVE('',#13029,#13030,#8016,.T.);
#17368=EDGE_CURVE('',#13030,#13030,#6259,.T.);
#17369=EDGE_CURVE('',#13031,#13032,#6260,.T.);
#17370=EDGE_CURVE('',#13032,#13033,#8017,.T.);
#17371=EDGE_CURVE('',#13033,#13034,#6261,.T.);
#17372=EDGE_CURVE('',#13031,#13034,#8018,.T.);
#17373=EDGE_CURVE('',#13032,#13035,#8019,.T.);
#17374=EDGE_CURVE('',#13035,#13036,#8020,.T.);
#17375=EDGE_CURVE('',#13036,#13033,#8021,.T.);
#17376=EDGE_CURVE('',#13035,#13037,#6262,.T.);
#17377=EDGE_CURVE('',#13037,#13038,#8022,.T.);
#17378=EDGE_CURVE('',#13038,#13036,#6263,.T.);
#17379=EDGE_CURVE('',#13037,#13004,#8023,.T.);
#17380=EDGE_CURVE('',#13003,#13038,#8024,.T.);
#17381=EDGE_CURVE('',#13001,#13031,#8025,.T.);
#17382=EDGE_CURVE('',#13034,#13002,#8026,.T.);
#17383=EDGE_CURVE('',#13039,#13039,#6264,.T.);
#17384=EDGE_CURVE('',#13040,#13040,#6265,.T.);
#17385=EDGE_CURVE('',#13041,#13042,#8027,.T.);
#17386=EDGE_CURVE('',#13042,#13043,#8028,.T.);
#17387=EDGE_CURVE('',#13043,#13044,#8029,.T.);
#17388=EDGE_CURVE('',#13041,#13044,#8030,.T.);
#17389=EDGE_CURVE('',#13042,#13045,#8031,.T.);
#17390=EDGE_CURVE('',#13045,#13046,#8032,.T.);
#17391=EDGE_CURVE('',#13046,#13043,#8033,.T.);
#17392=EDGE_CURVE('',#13045,#13047,#8034,.T.);
#17393=EDGE_CURVE('',#13047,#13048,#8035,.T.);
#17394=EDGE_CURVE('',#13048,#13046,#8036,.T.);
#17395=EDGE_CURVE('',#13047,#13049,#8037,.T.);
#17396=EDGE_CURVE('',#13049,#13050,#8038,.T.);
#17397=EDGE_CURVE('',#13050,#13048,#8039,.T.);
#17398=EDGE_CURVE('',#13049,#13051,#8040,.T.);
#17399=EDGE_CURVE('',#13051,#13052,#8041,.T.);
#17400=EDGE_CURVE('',#13052,#13050,#8042,.T.);
#17401=EDGE_CURVE('',#13051,#13053,#8043,.T.);
#17402=EDGE_CURVE('',#13053,#13054,#8044,.T.);
#17403=EDGE_CURVE('',#13054,#13052,#8045,.T.);
#17404=EDGE_CURVE('',#13053,#13041,#8046,.T.);
#17405=EDGE_CURVE('',#13044,#13054,#8047,.T.);
#17406=EDGE_CURVE('',#13055,#13055,#6266,.T.);
#17407=EDGE_CURVE('',#13055,#13056,#8048,.T.);
#17408=EDGE_CURVE('',#13056,#13056,#6267,.T.);
#17409=EDGE_CURVE('',#13039,#13057,#8049,.T.);
#17410=EDGE_CURVE('',#13057,#13057,#6268,.T.);
#17411=EDGE_CURVE('',#13040,#13058,#8050,.T.);
#17412=EDGE_CURVE('',#13058,#13058,#6269,.T.);
#17413=EDGE_CURVE('',#13059,#13060,#6270,.T.);
#17414=EDGE_CURVE('',#13060,#13061,#8051,.T.);
#17415=EDGE_CURVE('',#13062,#13061,#6271,.T.);
#17416=EDGE_CURVE('',#13059,#13062,#8052,.T.);
#17417=EDGE_CURVE('',#13063,#13059,#8053,.T.);
#17418=EDGE_CURVE('',#13064,#13062,#8054,.T.);
#17419=EDGE_CURVE('',#13063,#13064,#8055,.T.);
#17420=EDGE_CURVE('',#13065,#13063,#6272,.T.);
#17421=EDGE_CURVE('',#13066,#13064,#6273,.T.);
#17422=EDGE_CURVE('',#13065,#13066,#8056,.T.);
#17423=EDGE_CURVE('',#12993,#13065,#8057,.T.);
#17424=EDGE_CURVE('',#12994,#13066,#8058,.T.);
#17425=EDGE_CURVE('',#13060,#12996,#8059,.T.);
#17426=EDGE_CURVE('',#13061,#12995,#8060,.T.);
#17427=EDGE_CURVE('',#13067,#13067,#6274,.T.);
#17428=EDGE_CURVE('',#13068,#13068,#6275,.T.);
#17429=EDGE_CURVE('',#13069,#13070,#8061,.T.);
#17430=EDGE_CURVE('',#13070,#13071,#8062,.T.);
#17431=EDGE_CURVE('',#13072,#13071,#8063,.T.);
#17432=EDGE_CURVE('',#13069,#13072,#8064,.T.);
#17433=EDGE_CURVE('',#13073,#13069,#8065,.T.);
#17434=EDGE_CURVE('',#13074,#13072,#8066,.T.);
#17435=EDGE_CURVE('',#13073,#13074,#8067,.T.);
#17436=EDGE_CURVE('',#13075,#13073,#8068,.T.);
#17437=EDGE_CURVE('',#13076,#13074,#8069,.T.);
#17438=EDGE_CURVE('',#13075,#13076,#8070,.T.);
#17439=EDGE_CURVE('',#13077,#13075,#8071,.T.);
#17440=EDGE_CURVE('',#13078,#13076,#8072,.T.);
#17441=EDGE_CURVE('',#13077,#13078,#8073,.T.);
#17442=EDGE_CURVE('',#13079,#13077,#8074,.T.);
#17443=EDGE_CURVE('',#13080,#13078,#8075,.T.);
#17444=EDGE_CURVE('',#13079,#13080,#8076,.T.);
#17445=EDGE_CURVE('',#13081,#13079,#8077,.T.);
#17446=EDGE_CURVE('',#13082,#13080,#8078,.T.);
#17447=EDGE_CURVE('',#13081,#13082,#8079,.T.);
#17448=EDGE_CURVE('',#13070,#13081,#8080,.T.);
#17449=EDGE_CURVE('',#13071,#13082,#8081,.T.);
#17450=EDGE_CURVE('',#13083,#13083,#6276,.T.);
#17451=EDGE_CURVE('',#13083,#13084,#8082,.T.);
#17452=EDGE_CURVE('',#13084,#13084,#6277,.T.);
#17453=EDGE_CURVE('',#13085,#13086,#8083,.T.);
#17454=EDGE_CURVE('',#13086,#13087,#8084,.T.);
#17455=EDGE_CURVE('',#13088,#13087,#8085,.T.);
#17456=EDGE_CURVE('',#13085,#13088,#8086,.T.);
#17457=EDGE_CURVE('',#13089,#13085,#8087,.T.);
#17458=EDGE_CURVE('',#13090,#13088,#8088,.T.);
#17459=EDGE_CURVE('',#13089,#13090,#8089,.T.);
#17460=EDGE_CURVE('',#13091,#13089,#8090,.T.);
#17461=EDGE_CURVE('',#13092,#13090,#8091,.T.);
#17462=EDGE_CURVE('',#13091,#13092,#8092,.T.);
#17463=EDGE_CURVE('',#13093,#13091,#8093,.T.);
#17464=EDGE_CURVE('',#13094,#13092,#8094,.T.);
#17465=EDGE_CURVE('',#13093,#13094,#8095,.T.);
#17466=EDGE_CURVE('',#13095,#13093,#8096,.T.);
#17467=EDGE_CURVE('',#13096,#13094,#8097,.T.);
#17468=EDGE_CURVE('',#13095,#13096,#8098,.T.);
#17469=EDGE_CURVE('',#13097,#13095,#8099,.T.);
#17470=EDGE_CURVE('',#13098,#13096,#8100,.T.);
#17471=EDGE_CURVE('',#13097,#13098,#8101,.T.);
#17472=EDGE_CURVE('',#13086,#13097,#8102,.T.);
#17473=EDGE_CURVE('',#13087,#13098,#8103,.T.);
#17474=EDGE_CURVE('',#13099,#13099,#6278,.T.);
#17475=EDGE_CURVE('',#13099,#13100,#8104,.T.);
#17476=EDGE_CURVE('',#13100,#13100,#6279,.T.);
#17477=EDGE_CURVE('',#13101,#12992,#8105,.T.);
#17478=EDGE_CURVE('',#13101,#13102,#8106,.T.);
#17479=EDGE_CURVE('',#13102,#12997,#8107,.T.);
#17480=EDGE_CURVE('',#13103,#13103,#6280,.T.);
#17481=EDGE_CURVE('',#13103,#13068,#8108,.T.);
#17482=EDGE_CURVE('',#13104,#13104,#6281,.T.);
#17483=EDGE_CURVE('',#13104,#13067,#8109,.T.);
#17484=EDGE_CURVE('',#13105,#13105,#6282,.T.);
#17485=EDGE_CURVE('',#13105,#13013,#8110,.T.);
#17486=EDGE_CURVE('',#13106,#13106,#6283,.T.);
#17487=EDGE_CURVE('',#13106,#13014,#8111,.T.);
#17488=EDGE_CURVE('',#12985,#13107,#8112,.T.);
#17489=EDGE_CURVE('',#13107,#12976,#8113,.T.);
#17490=EDGE_CURVE('',#13107,#12982,#6284,.T.);
#17491=EDGE_CURVE('',#13108,#12983,#6285,.T.);
#17492=EDGE_CURVE('',#13108,#12986,#8114,.T.);
#17493=EDGE_CURVE('',#13108,#13109,#8115,.T.);
#17494=EDGE_CURVE('',#13109,#12987,#8116,.T.);
#17495=EDGE_CURVE('',#13109,#13110,#6286,.T.);
#17496=EDGE_CURVE('',#13110,#12988,#8117,.T.);
#17497=EDGE_CURVE('',#13110,#13111,#8118,.T.);
#17498=EDGE_CURVE('',#13111,#12989,#8119,.T.);
#17499=EDGE_CURVE('',#13111,#13112,#6287,.T.);
#17500=EDGE_CURVE('',#13112,#12990,#8120,.T.);
#17501=EDGE_CURVE('',#13112,#13113,#8121,.T.);
#17502=EDGE_CURVE('',#13113,#12991,#8122,.T.);
#17503=EDGE_CURVE('',#13113,#13101,#6288,.T.);
#17504=EDGE_CURVE('',#13102,#13114,#6289,.T.);
#17505=EDGE_CURVE('',#13114,#12998,#8123,.T.);
#17506=EDGE_CURVE('',#13114,#13115,#8124,.T.);
#17507=EDGE_CURVE('',#13115,#12999,#8125,.T.);
#17508=EDGE_CURVE('',#13115,#13116,#6290,.T.);
#17509=EDGE_CURVE('',#13116,#13000,#8126,.T.);
#17510=EDGE_CURVE('',#13117,#13116,#8127,.T.);
#17511=EDGE_CURVE('',#13117,#13005,#8128,.T.);
#17512=EDGE_CURVE('',#13117,#13118,#6291,.T.);
#17513=EDGE_CURVE('',#13118,#13006,#8129,.T.);
#17514=EDGE_CURVE('',#13119,#13118,#8130,.T.);
#17515=EDGE_CURVE('',#13119,#13007,#8131,.T.);
#17516=EDGE_CURVE('',#13119,#13120,#6292,.T.);
#17517=EDGE_CURVE('',#13120,#13008,#8132,.T.);
#17518=EDGE_CURVE('',#13121,#13120,#8133,.T.);
#17519=EDGE_CURVE('',#13121,#13009,#8134,.T.);
#17520=EDGE_CURVE('',#13121,#13122,#6293,.T.);
#17521=EDGE_CURVE('',#13122,#13010,#8135,.T.);
#17522=EDGE_CURVE('',#13123,#13122,#8136,.T.);
#17523=EDGE_CURVE('',#13123,#13011,#8137,.T.);
#17524=EDGE_CURVE('',#13124,#13123,#6294,.T.);
#17525=EDGE_CURVE('',#13124,#13012,#8138,.T.);
#17526=EDGE_CURVE('',#13125,#13124,#8139,.T.);
#17527=EDGE_CURVE('',#13125,#12966,#8140,.T.);
#17528=EDGE_CURVE('',#13125,#12980,#6295,.T.);
#23549=ORIENTED_EDGE('',*,*,#16136,.F.);
#23550=ORIENTED_EDGE('',*,*,#16137,.F.);
#23551=ORIENTED_EDGE('',*,*,#16138,.T.);
#23552=ORIENTED_EDGE('',*,*,#16139,.T.);
#23553=ORIENTED_EDGE('',*,*,#16140,.F.);
#23554=ORIENTED_EDGE('',*,*,#16141,.F.);
#23555=ORIENTED_EDGE('',*,*,#16142,.F.);
#23556=ORIENTED_EDGE('',*,*,#16136,.T.);
#23557=ORIENTED_EDGE('',*,*,#16143,.T.);
#23558=ORIENTED_EDGE('',*,*,#16144,.T.);
#23559=ORIENTED_EDGE('',*,*,#16145,.F.);
#23560=ORIENTED_EDGE('',*,*,#16146,.F.);
#23561=ORIENTED_EDGE('',*,*,#16147,.F.);
#23562=ORIENTED_EDGE('',*,*,#16140,.T.);
#23563=ORIENTED_EDGE('',*,*,#16148,.T.);
#23564=ORIENTED_EDGE('',*,*,#16149,.T.);
#23565=ORIENTED_EDGE('',*,*,#16150,.F.);
#23566=ORIENTED_EDGE('',*,*,#16151,.F.);
#23567=ORIENTED_EDGE('',*,*,#16152,.F.);
#23568=ORIENTED_EDGE('',*,*,#16145,.T.);
#23569=ORIENTED_EDGE('',*,*,#16153,.T.);
#23570=ORIENTED_EDGE('',*,*,#16154,.T.);
#23571=ORIENTED_EDGE('',*,*,#16155,.F.);
#23572=ORIENTED_EDGE('',*,*,#16156,.F.);
#23573=ORIENTED_EDGE('',*,*,#16157,.T.);
#23574=ORIENTED_EDGE('',*,*,#16158,.T.);
#23575=ORIENTED_EDGE('',*,*,#16159,.F.);
#23576=ORIENTED_EDGE('',*,*,#16160,.F.);
#23577=ORIENTED_EDGE('',*,*,#16161,.F.);
#23578=ORIENTED_EDGE('',*,*,#16155,.T.);
#23579=ORIENTED_EDGE('',*,*,#16162,.T.);
#23580=ORIENTED_EDGE('',*,*,#16163,.T.);
#23581=ORIENTED_EDGE('',*,*,#16164,.F.);
#23582=ORIENTED_EDGE('',*,*,#16165,.F.);
#23583=ORIENTED_EDGE('',*,*,#16166,.F.);
#23584=ORIENTED_EDGE('',*,*,#16159,.T.);
#23585=ORIENTED_EDGE('',*,*,#16167,.T.);
#23586=ORIENTED_EDGE('',*,*,#16168,.T.);
#23587=ORIENTED_EDGE('',*,*,#16169,.F.);
#23588=ORIENTED_EDGE('',*,*,#16170,.F.);
#23589=ORIENTED_EDGE('',*,*,#16171,.F.);
#23590=ORIENTED_EDGE('',*,*,#16164,.T.);
#23591=ORIENTED_EDGE('',*,*,#16172,.T.);
#23592=ORIENTED_EDGE('',*,*,#16173,.T.);
#23593=ORIENTED_EDGE('',*,*,#16174,.F.);
#23594=ORIENTED_EDGE('',*,*,#16175,.F.);
#23595=ORIENTED_EDGE('',*,*,#16176,.F.);
#23596=ORIENTED_EDGE('',*,*,#16177,.T.);
#23597=ORIENTED_EDGE('',*,*,#16178,.T.);
#23598=ORIENTED_EDGE('',*,*,#16179,.T.);
#23599=ORIENTED_EDGE('',*,*,#16180,.F.);
#23600=ORIENTED_EDGE('',*,*,#16181,.F.);
#23601=ORIENTED_EDGE('',*,*,#16182,.F.);
#23602=ORIENTED_EDGE('',*,*,#16174,.T.);
#23603=ORIENTED_EDGE('',*,*,#16183,.T.);
#23604=ORIENTED_EDGE('',*,*,#16184,.T.);
#23605=ORIENTED_EDGE('',*,*,#16185,.F.);
#23606=ORIENTED_EDGE('',*,*,#16186,.F.);
#23607=ORIENTED_EDGE('',*,*,#16187,.F.);
#23608=ORIENTED_EDGE('',*,*,#16180,.T.);
#23609=ORIENTED_EDGE('',*,*,#16188,.T.);
#23610=ORIENTED_EDGE('',*,*,#16189,.T.);
#23611=ORIENTED_EDGE('',*,*,#16190,.F.);
#23612=ORIENTED_EDGE('',*,*,#16191,.F.);
#23613=ORIENTED_EDGE('',*,*,#16192,.F.);
#23614=ORIENTED_EDGE('',*,*,#16185,.T.);
#23615=ORIENTED_EDGE('',*,*,#16193,.T.);
#23616=ORIENTED_EDGE('',*,*,#16194,.T.);
#23617=ORIENTED_EDGE('',*,*,#16195,.F.);
#23618=ORIENTED_EDGE('',*,*,#16196,.F.);
#23619=ORIENTED_EDGE('',*,*,#16197,.F.);
#23620=ORIENTED_EDGE('',*,*,#16190,.T.);
#23621=ORIENTED_EDGE('',*,*,#16198,.T.);
#23622=ORIENTED_EDGE('',*,*,#16199,.T.);
#23623=ORIENTED_EDGE('',*,*,#16200,.F.);
#23624=ORIENTED_EDGE('',*,*,#16201,.F.);
#23625=ORIENTED_EDGE('',*,*,#16202,.F.);
#23626=ORIENTED_EDGE('',*,*,#16195,.T.);
#23627=ORIENTED_EDGE('',*,*,#16203,.T.);
#23628=ORIENTED_EDGE('',*,*,#16204,.T.);
#23629=ORIENTED_EDGE('',*,*,#16205,.F.);
#23630=ORIENTED_EDGE('',*,*,#16206,.F.);
#23631=ORIENTED_EDGE('',*,*,#16207,.F.);
#23632=ORIENTED_EDGE('',*,*,#16200,.T.);
#23633=ORIENTED_EDGE('',*,*,#16208,.T.);
#23634=ORIENTED_EDGE('',*,*,#16209,.T.);
#23635=ORIENTED_EDGE('',*,*,#16210,.F.);
#23636=ORIENTED_EDGE('',*,*,#16211,.F.);
#23637=ORIENTED_EDGE('',*,*,#16212,.F.);
#23638=ORIENTED_EDGE('',*,*,#16205,.T.);
#23639=ORIENTED_EDGE('',*,*,#16213,.T.);
#23640=ORIENTED_EDGE('',*,*,#16214,.T.);
#23641=ORIENTED_EDGE('',*,*,#16215,.F.);
#23642=ORIENTED_EDGE('',*,*,#16216,.F.);
#23643=ORIENTED_EDGE('',*,*,#16217,.F.);
#23644=ORIENTED_EDGE('',*,*,#16210,.T.);
#23645=ORIENTED_EDGE('',*,*,#16218,.T.);
#23646=ORIENTED_EDGE('',*,*,#16219,.T.);
#23647=ORIENTED_EDGE('',*,*,#16220,.F.);
#23648=ORIENTED_EDGE('',*,*,#16221,.F.);
#23649=ORIENTED_EDGE('',*,*,#16222,.F.);
#23650=ORIENTED_EDGE('',*,*,#16215,.T.);
#23651=ORIENTED_EDGE('',*,*,#16223,.T.);
#23652=ORIENTED_EDGE('',*,*,#16224,.T.);
#23653=ORIENTED_EDGE('',*,*,#16225,.F.);
#23654=ORIENTED_EDGE('',*,*,#16226,.F.);
#23655=ORIENTED_EDGE('',*,*,#16227,.F.);
#23656=ORIENTED_EDGE('',*,*,#16220,.T.);
#23657=ORIENTED_EDGE('',*,*,#16228,.T.);
#23658=ORIENTED_EDGE('',*,*,#16229,.T.);
#23659=ORIENTED_EDGE('',*,*,#16230,.F.);
#23660=ORIENTED_EDGE('',*,*,#16231,.F.);
#23661=ORIENTED_EDGE('',*,*,#16232,.F.);
#23662=ORIENTED_EDGE('',*,*,#16225,.T.);
#23663=ORIENTED_EDGE('',*,*,#16233,.T.);
#23664=ORIENTED_EDGE('',*,*,#16234,.T.);
#23665=ORIENTED_EDGE('',*,*,#16235,.F.);
#23666=ORIENTED_EDGE('',*,*,#16236,.F.);
#23667=ORIENTED_EDGE('',*,*,#16237,.F.);
#23668=ORIENTED_EDGE('',*,*,#16230,.T.);
#23669=ORIENTED_EDGE('',*,*,#16238,.T.);
#23670=ORIENTED_EDGE('',*,*,#16239,.T.);
#23671=ORIENTED_EDGE('',*,*,#16240,.F.);
#23672=ORIENTED_EDGE('',*,*,#16241,.F.);
#23673=ORIENTED_EDGE('',*,*,#16242,.F.);
#23674=ORIENTED_EDGE('',*,*,#16235,.T.);
#23675=ORIENTED_EDGE('',*,*,#16243,.T.);
#23676=ORIENTED_EDGE('',*,*,#16244,.T.);
#23677=ORIENTED_EDGE('',*,*,#16245,.F.);
#23678=ORIENTED_EDGE('',*,*,#16246,.F.);
#23679=ORIENTED_EDGE('',*,*,#16247,.F.);
#23680=ORIENTED_EDGE('',*,*,#16240,.T.);
#23681=ORIENTED_EDGE('',*,*,#16248,.T.);
#23682=ORIENTED_EDGE('',*,*,#16249,.T.);
#23683=ORIENTED_EDGE('',*,*,#16250,.F.);
#23684=ORIENTED_EDGE('',*,*,#16251,.F.);
#23685=ORIENTED_EDGE('',*,*,#16252,.F.);
#23686=ORIENTED_EDGE('',*,*,#16245,.T.);
#23687=ORIENTED_EDGE('',*,*,#16253,.T.);
#23688=ORIENTED_EDGE('',*,*,#16254,.T.);
#23689=ORIENTED_EDGE('',*,*,#16255,.F.);
#23690=ORIENTED_EDGE('',*,*,#16256,.F.);
#23691=ORIENTED_EDGE('',*,*,#16257,.F.);
#23692=ORIENTED_EDGE('',*,*,#16250,.T.);
#23693=ORIENTED_EDGE('',*,*,#16258,.T.);
#23694=ORIENTED_EDGE('',*,*,#16259,.T.);
#23695=ORIENTED_EDGE('',*,*,#16260,.F.);
#23696=ORIENTED_EDGE('',*,*,#16261,.F.);
#23697=ORIENTED_EDGE('',*,*,#16262,.F.);
#23698=ORIENTED_EDGE('',*,*,#16255,.T.);
#23699=ORIENTED_EDGE('',*,*,#16263,.T.);
#23700=ORIENTED_EDGE('',*,*,#16264,.T.);
#23701=ORIENTED_EDGE('',*,*,#16265,.F.);
#23702=ORIENTED_EDGE('',*,*,#16266,.F.);
#23703=ORIENTED_EDGE('',*,*,#16267,.F.);
#23704=ORIENTED_EDGE('',*,*,#16260,.T.);
#23705=ORIENTED_EDGE('',*,*,#16268,.T.);
#23706=ORIENTED_EDGE('',*,*,#16269,.T.);
#23707=ORIENTED_EDGE('',*,*,#16270,.F.);
#23708=ORIENTED_EDGE('',*,*,#16271,.F.);
#23709=ORIENTED_EDGE('',*,*,#16272,.F.);
#23710=ORIENTED_EDGE('',*,*,#16265,.T.);
#23711=ORIENTED_EDGE('',*,*,#16273,.T.);
#23712=ORIENTED_EDGE('',*,*,#16274,.T.);
#23713=ORIENTED_EDGE('',*,*,#16275,.F.);
#23714=ORIENTED_EDGE('',*,*,#16276,.F.);
#23715=ORIENTED_EDGE('',*,*,#16277,.F.);
#23716=ORIENTED_EDGE('',*,*,#16270,.T.);
#23717=ORIENTED_EDGE('',*,*,#16278,.T.);
#23718=ORIENTED_EDGE('',*,*,#16279,.T.);
#23719=ORIENTED_EDGE('',*,*,#16280,.F.);
#23720=ORIENTED_EDGE('',*,*,#16281,.F.);
#23721=ORIENTED_EDGE('',*,*,#16282,.F.);
#23722=ORIENTED_EDGE('',*,*,#16275,.T.);
#23723=ORIENTED_EDGE('',*,*,#16283,.T.);
#23724=ORIENTED_EDGE('',*,*,#16284,.T.);
#23725=ORIENTED_EDGE('',*,*,#16285,.F.);
#23726=ORIENTED_EDGE('',*,*,#16286,.F.);
#23727=ORIENTED_EDGE('',*,*,#16287,.F.);
#23728=ORIENTED_EDGE('',*,*,#16280,.T.);
#23729=ORIENTED_EDGE('',*,*,#16288,.T.);
#23730=ORIENTED_EDGE('',*,*,#16289,.T.);
#23731=ORIENTED_EDGE('',*,*,#16290,.F.);
#23732=ORIENTED_EDGE('',*,*,#16291,.F.);
#23733=ORIENTED_EDGE('',*,*,#16292,.F.);
#23734=ORIENTED_EDGE('',*,*,#16285,.T.);
#23735=ORIENTED_EDGE('',*,*,#16293,.T.);
#23736=ORIENTED_EDGE('',*,*,#16294,.T.);
#23737=ORIENTED_EDGE('',*,*,#16295,.F.);
#23738=ORIENTED_EDGE('',*,*,#16296,.F.);
#23739=ORIENTED_EDGE('',*,*,#16297,.F.);
#23740=ORIENTED_EDGE('',*,*,#16290,.T.);
#23741=ORIENTED_EDGE('',*,*,#16298,.T.);
#23742=ORIENTED_EDGE('',*,*,#16299,.T.);
#23743=ORIENTED_EDGE('',*,*,#16300,.F.);
#23744=ORIENTED_EDGE('',*,*,#16301,.F.);
#23745=ORIENTED_EDGE('',*,*,#16302,.F.);
#23746=ORIENTED_EDGE('',*,*,#16295,.T.);
#23747=ORIENTED_EDGE('',*,*,#16303,.T.);
#23748=ORIENTED_EDGE('',*,*,#16304,.T.);
#23749=ORIENTED_EDGE('',*,*,#16305,.F.);
#23750=ORIENTED_EDGE('',*,*,#16306,.F.);
#23751=ORIENTED_EDGE('',*,*,#16307,.F.);
#23752=ORIENTED_EDGE('',*,*,#16300,.T.);
#23753=ORIENTED_EDGE('',*,*,#16308,.T.);
#23754=ORIENTED_EDGE('',*,*,#16309,.T.);
#23755=ORIENTED_EDGE('',*,*,#16310,.F.);
#23756=ORIENTED_EDGE('',*,*,#16311,.F.);
#23757=ORIENTED_EDGE('',*,*,#16312,.F.);
#23758=ORIENTED_EDGE('',*,*,#16313,.T.);
#23759=ORIENTED_EDGE('',*,*,#16314,.T.);
#23760=ORIENTED_EDGE('',*,*,#16315,.T.);
#23761=ORIENTED_EDGE('',*,*,#16316,.F.);
#23762=ORIENTED_EDGE('',*,*,#16317,.F.);
#23763=ORIENTED_EDGE('',*,*,#16318,.F.);
#23764=ORIENTED_EDGE('',*,*,#16310,.T.);
#23765=ORIENTED_EDGE('',*,*,#16319,.T.);
#23766=ORIENTED_EDGE('',*,*,#16320,.T.);
#23767=ORIENTED_EDGE('',*,*,#16321,.F.);
#23768=ORIENTED_EDGE('',*,*,#16322,.F.);
#23769=ORIENTED_EDGE('',*,*,#16323,.F.);
#23770=ORIENTED_EDGE('',*,*,#16316,.T.);
#23771=ORIENTED_EDGE('',*,*,#16324,.T.);
#23772=ORIENTED_EDGE('',*,*,#16325,.T.);
#23773=ORIENTED_EDGE('',*,*,#16326,.F.);
#23774=ORIENTED_EDGE('',*,*,#16327,.F.);
#23775=ORIENTED_EDGE('',*,*,#16328,.F.);
#23776=ORIENTED_EDGE('',*,*,#16321,.T.);
#23777=ORIENTED_EDGE('',*,*,#16329,.T.);
#23778=ORIENTED_EDGE('',*,*,#16330,.T.);
#23779=ORIENTED_EDGE('',*,*,#16331,.F.);
#23780=ORIENTED_EDGE('',*,*,#16332,.F.);
#23781=ORIENTED_EDGE('',*,*,#16333,.F.);
#23782=ORIENTED_EDGE('',*,*,#16326,.T.);
#23783=ORIENTED_EDGE('',*,*,#16334,.T.);
#23784=ORIENTED_EDGE('',*,*,#16335,.T.);
#23785=ORIENTED_EDGE('',*,*,#16336,.F.);
#23786=ORIENTED_EDGE('',*,*,#16337,.F.);
#23787=ORIENTED_EDGE('',*,*,#16338,.F.);
#23788=ORIENTED_EDGE('',*,*,#16331,.T.);
#23789=ORIENTED_EDGE('',*,*,#16339,.T.);
#23790=ORIENTED_EDGE('',*,*,#16340,.T.);
#23791=ORIENTED_EDGE('',*,*,#16341,.F.);
#23792=ORIENTED_EDGE('',*,*,#16342,.F.);
#23793=ORIENTED_EDGE('',*,*,#16343,.F.);
#23794=ORIENTED_EDGE('',*,*,#16336,.T.);
#23795=ORIENTED_EDGE('',*,*,#16344,.T.);
#23796=ORIENTED_EDGE('',*,*,#16345,.T.);
#23797=ORIENTED_EDGE('',*,*,#16346,.F.);
#23798=ORIENTED_EDGE('',*,*,#16347,.F.);
#23799=ORIENTED_EDGE('',*,*,#16348,.F.);
#23800=ORIENTED_EDGE('',*,*,#16341,.T.);
#23801=ORIENTED_EDGE('',*,*,#16349,.T.);
#23802=ORIENTED_EDGE('',*,*,#16350,.T.);
#23803=ORIENTED_EDGE('',*,*,#16351,.F.);
#23804=ORIENTED_EDGE('',*,*,#16352,.F.);
#23805=ORIENTED_EDGE('',*,*,#16353,.F.);
#23806=ORIENTED_EDGE('',*,*,#16346,.T.);
#23807=ORIENTED_EDGE('',*,*,#16354,.T.);
#23808=ORIENTED_EDGE('',*,*,#16355,.T.);
#23809=ORIENTED_EDGE('',*,*,#16356,.F.);
#23810=ORIENTED_EDGE('',*,*,#16357,.F.);
#23811=ORIENTED_EDGE('',*,*,#16358,.F.);
#23812=ORIENTED_EDGE('',*,*,#16351,.T.);
#23813=ORIENTED_EDGE('',*,*,#16359,.T.);
#23814=ORIENTED_EDGE('',*,*,#16360,.T.);
#23815=ORIENTED_EDGE('',*,*,#16361,.F.);
#23816=ORIENTED_EDGE('',*,*,#16362,.F.);
#23817=ORIENTED_EDGE('',*,*,#16363,.F.);
#23818=ORIENTED_EDGE('',*,*,#16356,.T.);
#23819=ORIENTED_EDGE('',*,*,#16364,.T.);
#23820=ORIENTED_EDGE('',*,*,#16365,.T.);
#23821=ORIENTED_EDGE('',*,*,#16366,.F.);
#23822=ORIENTED_EDGE('',*,*,#16367,.F.);
#23823=ORIENTED_EDGE('',*,*,#16368,.F.);
#23824=ORIENTED_EDGE('',*,*,#16361,.T.);
#23825=ORIENTED_EDGE('',*,*,#16369,.T.);
#23826=ORIENTED_EDGE('',*,*,#16370,.T.);
#23827=ORIENTED_EDGE('',*,*,#16371,.F.);
#23828=ORIENTED_EDGE('',*,*,#16372,.F.);
#23829=ORIENTED_EDGE('',*,*,#16373,.F.);
#23830=ORIENTED_EDGE('',*,*,#16366,.T.);
#23831=ORIENTED_EDGE('',*,*,#16374,.T.);
#23832=ORIENTED_EDGE('',*,*,#16375,.T.);
#23833=ORIENTED_EDGE('',*,*,#16376,.F.);
#23834=ORIENTED_EDGE('',*,*,#16377,.F.);
#23835=ORIENTED_EDGE('',*,*,#16378,.F.);
#23836=ORIENTED_EDGE('',*,*,#16371,.T.);
#23837=ORIENTED_EDGE('',*,*,#16379,.T.);
#23838=ORIENTED_EDGE('',*,*,#16380,.T.);
#23839=ORIENTED_EDGE('',*,*,#16381,.F.);
#23840=ORIENTED_EDGE('',*,*,#16382,.F.);
#23841=ORIENTED_EDGE('',*,*,#16383,.F.);
#23842=ORIENTED_EDGE('',*,*,#16376,.T.);
#23843=ORIENTED_EDGE('',*,*,#16384,.T.);
#23844=ORIENTED_EDGE('',*,*,#16385,.T.);
#23845=ORIENTED_EDGE('',*,*,#16386,.F.);
#23846=ORIENTED_EDGE('',*,*,#16387,.F.);
#23847=ORIENTED_EDGE('',*,*,#16388,.F.);
#23848=ORIENTED_EDGE('',*,*,#16381,.T.);
#23849=ORIENTED_EDGE('',*,*,#16389,.T.);
#23850=ORIENTED_EDGE('',*,*,#16390,.T.);
#23851=ORIENTED_EDGE('',*,*,#16391,.F.);
#23852=ORIENTED_EDGE('',*,*,#16392,.F.);
#23853=ORIENTED_EDGE('',*,*,#16393,.F.);
#23854=ORIENTED_EDGE('',*,*,#16386,.T.);
#23855=ORIENTED_EDGE('',*,*,#16394,.T.);
#23856=ORIENTED_EDGE('',*,*,#16395,.T.);
#23857=ORIENTED_EDGE('',*,*,#16396,.F.);
#23858=ORIENTED_EDGE('',*,*,#16397,.F.);
#23859=ORIENTED_EDGE('',*,*,#16398,.F.);
#23860=ORIENTED_EDGE('',*,*,#16391,.T.);
#23861=ORIENTED_EDGE('',*,*,#16399,.T.);
#23862=ORIENTED_EDGE('',*,*,#16400,.T.);
#23863=ORIENTED_EDGE('',*,*,#16401,.F.);
#23864=ORIENTED_EDGE('',*,*,#16402,.F.);
#23865=ORIENTED_EDGE('',*,*,#16403,.F.);
#23866=ORIENTED_EDGE('',*,*,#16396,.T.);
#23867=ORIENTED_EDGE('',*,*,#16404,.T.);
#23868=ORIENTED_EDGE('',*,*,#16405,.T.);
#23869=ORIENTED_EDGE('',*,*,#16406,.F.);
#23870=ORIENTED_EDGE('',*,*,#16407,.F.);
#23871=ORIENTED_EDGE('',*,*,#16408,.F.);
#23872=ORIENTED_EDGE('',*,*,#16401,.T.);
#23873=ORIENTED_EDGE('',*,*,#16409,.T.);
#23874=ORIENTED_EDGE('',*,*,#16410,.T.);
#23875=ORIENTED_EDGE('',*,*,#16411,.F.);
#23876=ORIENTED_EDGE('',*,*,#16412,.F.);
#23877=ORIENTED_EDGE('',*,*,#16413,.F.);
#23878=ORIENTED_EDGE('',*,*,#16406,.T.);
#23879=ORIENTED_EDGE('',*,*,#16414,.T.);
#23880=ORIENTED_EDGE('',*,*,#16415,.T.);
#23881=ORIENTED_EDGE('',*,*,#16416,.F.);
#23882=ORIENTED_EDGE('',*,*,#16417,.F.);
#23883=ORIENTED_EDGE('',*,*,#16418,.F.);
#23884=ORIENTED_EDGE('',*,*,#16411,.T.);
#23885=ORIENTED_EDGE('',*,*,#16419,.T.);
#23886=ORIENTED_EDGE('',*,*,#16420,.T.);
#23887=ORIENTED_EDGE('',*,*,#16421,.F.);
#23888=ORIENTED_EDGE('',*,*,#16422,.F.);
#23889=ORIENTED_EDGE('',*,*,#16423,.F.);
#23890=ORIENTED_EDGE('',*,*,#16416,.T.);
#23891=ORIENTED_EDGE('',*,*,#16424,.T.);
#23892=ORIENTED_EDGE('',*,*,#16425,.T.);
#23893=ORIENTED_EDGE('',*,*,#16426,.F.);
#23894=ORIENTED_EDGE('',*,*,#16427,.F.);
#23895=ORIENTED_EDGE('',*,*,#16428,.F.);
#23896=ORIENTED_EDGE('',*,*,#16421,.T.);
#23897=ORIENTED_EDGE('',*,*,#16429,.T.);
#23898=ORIENTED_EDGE('',*,*,#16430,.T.);
#23899=ORIENTED_EDGE('',*,*,#16431,.F.);
#23900=ORIENTED_EDGE('',*,*,#16432,.F.);
#23901=ORIENTED_EDGE('',*,*,#16433,.F.);
#23902=ORIENTED_EDGE('',*,*,#16426,.T.);
#23903=ORIENTED_EDGE('',*,*,#16434,.T.);
#23904=ORIENTED_EDGE('',*,*,#16435,.T.);
#23905=ORIENTED_EDGE('',*,*,#16436,.F.);
#23906=ORIENTED_EDGE('',*,*,#16437,.F.);
#23907=ORIENTED_EDGE('',*,*,#16438,.F.);
#23908=ORIENTED_EDGE('',*,*,#16431,.T.);
#23909=ORIENTED_EDGE('',*,*,#16439,.T.);
#23910=ORIENTED_EDGE('',*,*,#16440,.T.);
#23911=ORIENTED_EDGE('',*,*,#16441,.F.);
#23912=ORIENTED_EDGE('',*,*,#16442,.F.);
#23913=ORIENTED_EDGE('',*,*,#16443,.F.);
#23914=ORIENTED_EDGE('',*,*,#16436,.T.);
#23915=ORIENTED_EDGE('',*,*,#16444,.T.);
#23916=ORIENTED_EDGE('',*,*,#16445,.T.);
#23917=ORIENTED_EDGE('',*,*,#16446,.F.);
#23918=ORIENTED_EDGE('',*,*,#16447,.F.);
#23919=ORIENTED_EDGE('',*,*,#16448,.F.);
#23920=ORIENTED_EDGE('',*,*,#16449,.T.);
#23921=ORIENTED_EDGE('',*,*,#16450,.T.);
#23922=ORIENTED_EDGE('',*,*,#16451,.T.);
#23923=ORIENTED_EDGE('',*,*,#16452,.F.);
#23924=ORIENTED_EDGE('',*,*,#16453,.F.);
#23925=ORIENTED_EDGE('',*,*,#16454,.F.);
#23926=ORIENTED_EDGE('',*,*,#16446,.T.);
#23927=ORIENTED_EDGE('',*,*,#16455,.T.);
#23928=ORIENTED_EDGE('',*,*,#16456,.T.);
#23929=ORIENTED_EDGE('',*,*,#16457,.F.);
#23930=ORIENTED_EDGE('',*,*,#16458,.F.);
#23931=ORIENTED_EDGE('',*,*,#16459,.F.);
#23932=ORIENTED_EDGE('',*,*,#16452,.T.);
#23933=ORIENTED_EDGE('',*,*,#16460,.T.);
#23934=ORIENTED_EDGE('',*,*,#16461,.T.);
#23935=ORIENTED_EDGE('',*,*,#16462,.F.);
#23936=ORIENTED_EDGE('',*,*,#16463,.F.);
#23937=ORIENTED_EDGE('',*,*,#16464,.F.);
#23938=ORIENTED_EDGE('',*,*,#16457,.T.);
#23939=ORIENTED_EDGE('',*,*,#16465,.T.);
#23940=ORIENTED_EDGE('',*,*,#16466,.T.);
#23941=ORIENTED_EDGE('',*,*,#16467,.F.);
#23942=ORIENTED_EDGE('',*,*,#16468,.F.);
#23943=ORIENTED_EDGE('',*,*,#16469,.F.);
#23944=ORIENTED_EDGE('',*,*,#16462,.T.);
#23945=ORIENTED_EDGE('',*,*,#16470,.T.);
#23946=ORIENTED_EDGE('',*,*,#16471,.T.);
#23947=ORIENTED_EDGE('',*,*,#16472,.F.);
#23948=ORIENTED_EDGE('',*,*,#16473,.F.);
#23949=ORIENTED_EDGE('',*,*,#16474,.F.);
#23950=ORIENTED_EDGE('',*,*,#16467,.T.);
#23951=ORIENTED_EDGE('',*,*,#16475,.T.);
#23952=ORIENTED_EDGE('',*,*,#16476,.T.);
#23953=ORIENTED_EDGE('',*,*,#16477,.F.);
#23954=ORIENTED_EDGE('',*,*,#16478,.F.);
#23955=ORIENTED_EDGE('',*,*,#16479,.F.);
#23956=ORIENTED_EDGE('',*,*,#16472,.T.);
#23957=ORIENTED_EDGE('',*,*,#16480,.T.);
#23958=ORIENTED_EDGE('',*,*,#16481,.T.);
#23959=ORIENTED_EDGE('',*,*,#16482,.F.);
#23960=ORIENTED_EDGE('',*,*,#16483,.F.);
#23961=ORIENTED_EDGE('',*,*,#16484,.F.);
#23962=ORIENTED_EDGE('',*,*,#16477,.T.);
#23963=ORIENTED_EDGE('',*,*,#16485,.T.);
#23964=ORIENTED_EDGE('',*,*,#16486,.T.);
#23965=ORIENTED_EDGE('',*,*,#16487,.F.);
#23966=ORIENTED_EDGE('',*,*,#16488,.F.);
#23967=ORIENTED_EDGE('',*,*,#16489,.F.);
#23968=ORIENTED_EDGE('',*,*,#16482,.T.);
#23969=ORIENTED_EDGE('',*,*,#16490,.T.);
#23970=ORIENTED_EDGE('',*,*,#16491,.T.);
#23971=ORIENTED_EDGE('',*,*,#16492,.F.);
#23972=ORIENTED_EDGE('',*,*,#16493,.F.);
#23973=ORIENTED_EDGE('',*,*,#16494,.F.);
#23974=ORIENTED_EDGE('',*,*,#16487,.T.);
#23975=ORIENTED_EDGE('',*,*,#16495,.T.);
#23976=ORIENTED_EDGE('',*,*,#16496,.T.);
#23977=ORIENTED_EDGE('',*,*,#16497,.F.);
#23978=ORIENTED_EDGE('',*,*,#16498,.F.);
#23979=ORIENTED_EDGE('',*,*,#16499,.F.);
#23980=ORIENTED_EDGE('',*,*,#16492,.T.);
#23981=ORIENTED_EDGE('',*,*,#16500,.T.);
#23982=ORIENTED_EDGE('',*,*,#16501,.T.);
#23983=ORIENTED_EDGE('',*,*,#16502,.F.);
#23984=ORIENTED_EDGE('',*,*,#16503,.F.);
#23985=ORIENTED_EDGE('',*,*,#16504,.F.);
#23986=ORIENTED_EDGE('',*,*,#16497,.T.);
#23987=ORIENTED_EDGE('',*,*,#16505,.T.);
#23988=ORIENTED_EDGE('',*,*,#16506,.T.);
#23989=ORIENTED_EDGE('',*,*,#16507,.F.);
#23990=ORIENTED_EDGE('',*,*,#16508,.F.);
#23991=ORIENTED_EDGE('',*,*,#16509,.F.);
#23992=ORIENTED_EDGE('',*,*,#16502,.T.);
#23993=ORIENTED_EDGE('',*,*,#16510,.T.);
#23994=ORIENTED_EDGE('',*,*,#16511,.T.);
#23995=ORIENTED_EDGE('',*,*,#16512,.F.);
#23996=ORIENTED_EDGE('',*,*,#16513,.F.);
#23997=ORIENTED_EDGE('',*,*,#16514,.F.);
#23998=ORIENTED_EDGE('',*,*,#16507,.T.);
#23999=ORIENTED_EDGE('',*,*,#16515,.T.);
#24000=ORIENTED_EDGE('',*,*,#16516,.T.);
#24001=ORIENTED_EDGE('',*,*,#16517,.F.);
#24002=ORIENTED_EDGE('',*,*,#16518,.F.);
#24003=ORIENTED_EDGE('',*,*,#16519,.F.);
#24004=ORIENTED_EDGE('',*,*,#16512,.T.);
#24005=ORIENTED_EDGE('',*,*,#16520,.T.);
#24006=ORIENTED_EDGE('',*,*,#16521,.T.);
#24007=ORIENTED_EDGE('',*,*,#16522,.F.);
#24008=ORIENTED_EDGE('',*,*,#16523,.F.);
#24009=ORIENTED_EDGE('',*,*,#16524,.F.);
#24010=ORIENTED_EDGE('',*,*,#16517,.T.);
#24011=ORIENTED_EDGE('',*,*,#16525,.T.);
#24012=ORIENTED_EDGE('',*,*,#16526,.T.);
#24013=ORIENTED_EDGE('',*,*,#16527,.F.);
#24014=ORIENTED_EDGE('',*,*,#16528,.F.);
#24015=ORIENTED_EDGE('',*,*,#16529,.F.);
#24016=ORIENTED_EDGE('',*,*,#16522,.T.);
#24017=ORIENTED_EDGE('',*,*,#16530,.T.);
#24018=ORIENTED_EDGE('',*,*,#16531,.T.);
#24019=ORIENTED_EDGE('',*,*,#16532,.F.);
#24020=ORIENTED_EDGE('',*,*,#16533,.F.);
#24021=ORIENTED_EDGE('',*,*,#16534,.F.);
#24022=ORIENTED_EDGE('',*,*,#16527,.T.);
#24023=ORIENTED_EDGE('',*,*,#16535,.T.);
#24024=ORIENTED_EDGE('',*,*,#16536,.T.);
#24025=ORIENTED_EDGE('',*,*,#16537,.F.);
#24026=ORIENTED_EDGE('',*,*,#16538,.F.);
#24027=ORIENTED_EDGE('',*,*,#16539,.F.);
#24028=ORIENTED_EDGE('',*,*,#16532,.T.);
#24029=ORIENTED_EDGE('',*,*,#16540,.T.);
#24030=ORIENTED_EDGE('',*,*,#16541,.T.);
#24031=ORIENTED_EDGE('',*,*,#16542,.F.);
#24032=ORIENTED_EDGE('',*,*,#16543,.F.);
#24033=ORIENTED_EDGE('',*,*,#16544,.F.);
#24034=ORIENTED_EDGE('',*,*,#16537,.T.);
#24035=ORIENTED_EDGE('',*,*,#16545,.T.);
#24036=ORIENTED_EDGE('',*,*,#16546,.T.);
#24037=ORIENTED_EDGE('',*,*,#16547,.F.);
#24038=ORIENTED_EDGE('',*,*,#16548,.F.);
#24039=ORIENTED_EDGE('',*,*,#16549,.F.);
#24040=ORIENTED_EDGE('',*,*,#16542,.T.);
#24041=ORIENTED_EDGE('',*,*,#16550,.T.);
#24042=ORIENTED_EDGE('',*,*,#16551,.T.);
#24043=ORIENTED_EDGE('',*,*,#16552,.F.);
#24044=ORIENTED_EDGE('',*,*,#16553,.F.);
#24045=ORIENTED_EDGE('',*,*,#16554,.F.);
#24046=ORIENTED_EDGE('',*,*,#16547,.T.);
#24047=ORIENTED_EDGE('',*,*,#16555,.T.);
#24048=ORIENTED_EDGE('',*,*,#16556,.T.);
#24049=ORIENTED_EDGE('',*,*,#16557,.F.);
#24050=ORIENTED_EDGE('',*,*,#16558,.F.);
#24051=ORIENTED_EDGE('',*,*,#16559,.F.);
#24052=ORIENTED_EDGE('',*,*,#16552,.T.);
#24053=ORIENTED_EDGE('',*,*,#16560,.T.);
#24054=ORIENTED_EDGE('',*,*,#16561,.T.);
#24055=ORIENTED_EDGE('',*,*,#16562,.F.);
#24056=ORIENTED_EDGE('',*,*,#16563,.F.);
#24057=ORIENTED_EDGE('',*,*,#16564,.F.);
#24058=ORIENTED_EDGE('',*,*,#16557,.T.);
#24059=ORIENTED_EDGE('',*,*,#16565,.T.);
#24060=ORIENTED_EDGE('',*,*,#16566,.T.);
#24061=ORIENTED_EDGE('',*,*,#16567,.F.);
#24062=ORIENTED_EDGE('',*,*,#16568,.F.);
#24063=ORIENTED_EDGE('',*,*,#16569,.F.);
#24064=ORIENTED_EDGE('',*,*,#16562,.T.);
#24065=ORIENTED_EDGE('',*,*,#16570,.T.);
#24066=ORIENTED_EDGE('',*,*,#16571,.T.);
#24067=ORIENTED_EDGE('',*,*,#16572,.F.);
#24068=ORIENTED_EDGE('',*,*,#16573,.F.);
#24069=ORIENTED_EDGE('',*,*,#16574,.F.);
#24070=ORIENTED_EDGE('',*,*,#16567,.T.);
#24071=ORIENTED_EDGE('',*,*,#16575,.T.);
#24072=ORIENTED_EDGE('',*,*,#16576,.T.);
#24073=ORIENTED_EDGE('',*,*,#16577,.F.);
#24074=ORIENTED_EDGE('',*,*,#16578,.F.);
#24075=ORIENTED_EDGE('',*,*,#16579,.F.);
#24076=ORIENTED_EDGE('',*,*,#16572,.T.);
#24077=ORIENTED_EDGE('',*,*,#16580,.T.);
#24078=ORIENTED_EDGE('',*,*,#16581,.T.);
#24079=ORIENTED_EDGE('',*,*,#16582,.F.);
#24080=ORIENTED_EDGE('',*,*,#16583,.F.);
#24081=ORIENTED_EDGE('',*,*,#16584,.F.);
#24082=ORIENTED_EDGE('',*,*,#16585,.T.);
#24083=ORIENTED_EDGE('',*,*,#16586,.T.);
#24084=ORIENTED_EDGE('',*,*,#16587,.T.);
#24085=ORIENTED_EDGE('',*,*,#16588,.F.);
#24086=ORIENTED_EDGE('',*,*,#16589,.F.);
#24087=ORIENTED_EDGE('',*,*,#16590,.F.);
#24088=ORIENTED_EDGE('',*,*,#16582,.T.);
#24089=ORIENTED_EDGE('',*,*,#16591,.T.);
#24090=ORIENTED_EDGE('',*,*,#16592,.T.);
#24091=ORIENTED_EDGE('',*,*,#16593,.F.);
#24092=ORIENTED_EDGE('',*,*,#16594,.F.);
#24093=ORIENTED_EDGE('',*,*,#16595,.F.);
#24094=ORIENTED_EDGE('',*,*,#16588,.T.);
#24095=ORIENTED_EDGE('',*,*,#16596,.T.);
#24096=ORIENTED_EDGE('',*,*,#16597,.T.);
#24097=ORIENTED_EDGE('',*,*,#16598,.F.);
#24098=ORIENTED_EDGE('',*,*,#16599,.F.);
#24099=ORIENTED_EDGE('',*,*,#16600,.F.);
#24100=ORIENTED_EDGE('',*,*,#16593,.T.);
#24101=ORIENTED_EDGE('',*,*,#16601,.T.);
#24102=ORIENTED_EDGE('',*,*,#16602,.T.);
#24103=ORIENTED_EDGE('',*,*,#16603,.F.);
#24104=ORIENTED_EDGE('',*,*,#16604,.F.);
#24105=ORIENTED_EDGE('',*,*,#16605,.F.);
#24106=ORIENTED_EDGE('',*,*,#16598,.T.);
#24107=ORIENTED_EDGE('',*,*,#16606,.T.);
#24108=ORIENTED_EDGE('',*,*,#16607,.T.);
#24109=ORIENTED_EDGE('',*,*,#16608,.F.);
#24110=ORIENTED_EDGE('',*,*,#16609,.F.);
#24111=ORIENTED_EDGE('',*,*,#16610,.F.);
#24112=ORIENTED_EDGE('',*,*,#16603,.T.);
#24113=ORIENTED_EDGE('',*,*,#16611,.T.);
#24114=ORIENTED_EDGE('',*,*,#16612,.T.);
#24115=ORIENTED_EDGE('',*,*,#16613,.F.);
#24116=ORIENTED_EDGE('',*,*,#16614,.F.);
#24117=ORIENTED_EDGE('',*,*,#16615,.F.);
#24118=ORIENTED_EDGE('',*,*,#16608,.T.);
#24119=ORIENTED_EDGE('',*,*,#16616,.T.);
#24120=ORIENTED_EDGE('',*,*,#16617,.T.);
#24121=ORIENTED_EDGE('',*,*,#16618,.F.);
#24122=ORIENTED_EDGE('',*,*,#16619,.F.);
#24123=ORIENTED_EDGE('',*,*,#16620,.F.);
#24124=ORIENTED_EDGE('',*,*,#16613,.T.);
#24125=ORIENTED_EDGE('',*,*,#16621,.T.);
#24126=ORIENTED_EDGE('',*,*,#16622,.T.);
#24127=ORIENTED_EDGE('',*,*,#16623,.F.);
#24128=ORIENTED_EDGE('',*,*,#16624,.F.);
#24129=ORIENTED_EDGE('',*,*,#16625,.F.);
#24130=ORIENTED_EDGE('',*,*,#16618,.T.);
#24131=ORIENTED_EDGE('',*,*,#16626,.T.);
#24132=ORIENTED_EDGE('',*,*,#16627,.T.);
#24133=ORIENTED_EDGE('',*,*,#16628,.F.);
#24134=ORIENTED_EDGE('',*,*,#16629,.F.);
#24135=ORIENTED_EDGE('',*,*,#16630,.F.);
#24136=ORIENTED_EDGE('',*,*,#16623,.T.);
#24137=ORIENTED_EDGE('',*,*,#16631,.T.);
#24138=ORIENTED_EDGE('',*,*,#16632,.T.);
#24139=ORIENTED_EDGE('',*,*,#16633,.F.);
#24140=ORIENTED_EDGE('',*,*,#16634,.F.);
#24141=ORIENTED_EDGE('',*,*,#16635,.F.);
#24142=ORIENTED_EDGE('',*,*,#16628,.T.);
#24143=ORIENTED_EDGE('',*,*,#16636,.T.);
#24144=ORIENTED_EDGE('',*,*,#16637,.T.);
#24145=ORIENTED_EDGE('',*,*,#16638,.F.);
#24146=ORIENTED_EDGE('',*,*,#16639,.F.);
#24147=ORIENTED_EDGE('',*,*,#16640,.F.);
#24148=ORIENTED_EDGE('',*,*,#16633,.T.);
#24149=ORIENTED_EDGE('',*,*,#16641,.T.);
#24150=ORIENTED_EDGE('',*,*,#16642,.T.);
#24151=ORIENTED_EDGE('',*,*,#16643,.F.);
#24152=ORIENTED_EDGE('',*,*,#16644,.F.);
#24153=ORIENTED_EDGE('',*,*,#16645,.F.);
#24154=ORIENTED_EDGE('',*,*,#16638,.T.);
#24155=ORIENTED_EDGE('',*,*,#16646,.T.);
#24156=ORIENTED_EDGE('',*,*,#16647,.T.);
#24157=ORIENTED_EDGE('',*,*,#16648,.F.);
#24158=ORIENTED_EDGE('',*,*,#16649,.F.);
#24159=ORIENTED_EDGE('',*,*,#16650,.F.);
#24160=ORIENTED_EDGE('',*,*,#16643,.T.);
#24161=ORIENTED_EDGE('',*,*,#16651,.T.);
#24162=ORIENTED_EDGE('',*,*,#16652,.T.);
#24163=ORIENTED_EDGE('',*,*,#16653,.F.);
#24164=ORIENTED_EDGE('',*,*,#16654,.F.);
#24165=ORIENTED_EDGE('',*,*,#16655,.F.);
#24166=ORIENTED_EDGE('',*,*,#16648,.T.);
#24167=ORIENTED_EDGE('',*,*,#16656,.T.);
#24168=ORIENTED_EDGE('',*,*,#16657,.T.);
#24169=ORIENTED_EDGE('',*,*,#16658,.F.);
#24170=ORIENTED_EDGE('',*,*,#16659,.F.);
#24171=ORIENTED_EDGE('',*,*,#16660,.F.);
#24172=ORIENTED_EDGE('',*,*,#16653,.T.);
#24173=ORIENTED_EDGE('',*,*,#16661,.T.);
#24174=ORIENTED_EDGE('',*,*,#16662,.T.);
#24175=ORIENTED_EDGE('',*,*,#16663,.F.);
#24176=ORIENTED_EDGE('',*,*,#16664,.F.);
#24177=ORIENTED_EDGE('',*,*,#16665,.F.);
#24178=ORIENTED_EDGE('',*,*,#16658,.T.);
#24179=ORIENTED_EDGE('',*,*,#16666,.T.);
#24180=ORIENTED_EDGE('',*,*,#16667,.T.);
#24181=ORIENTED_EDGE('',*,*,#16668,.F.);
#24182=ORIENTED_EDGE('',*,*,#16669,.F.);
#24183=ORIENTED_EDGE('',*,*,#16670,.F.);
#24184=ORIENTED_EDGE('',*,*,#16663,.T.);
#24185=ORIENTED_EDGE('',*,*,#16671,.T.);
#24186=ORIENTED_EDGE('',*,*,#16672,.T.);
#24187=ORIENTED_EDGE('',*,*,#16673,.F.);
#24188=ORIENTED_EDGE('',*,*,#16674,.F.);
#24189=ORIENTED_EDGE('',*,*,#16675,.F.);
#24190=ORIENTED_EDGE('',*,*,#16668,.T.);
#24191=ORIENTED_EDGE('',*,*,#16676,.T.);
#24192=ORIENTED_EDGE('',*,*,#16677,.T.);
#24193=ORIENTED_EDGE('',*,*,#16678,.F.);
#24194=ORIENTED_EDGE('',*,*,#16679,.F.);
#24195=ORIENTED_EDGE('',*,*,#16680,.F.);
#24196=ORIENTED_EDGE('',*,*,#16673,.T.);
#24197=ORIENTED_EDGE('',*,*,#16681,.T.);
#24198=ORIENTED_EDGE('',*,*,#16682,.T.);
#24199=ORIENTED_EDGE('',*,*,#16683,.F.);
#24200=ORIENTED_EDGE('',*,*,#16684,.F.);
#24201=ORIENTED_EDGE('',*,*,#16685,.F.);
#24202=ORIENTED_EDGE('',*,*,#16678,.T.);
#24203=ORIENTED_EDGE('',*,*,#16686,.T.);
#24204=ORIENTED_EDGE('',*,*,#16687,.T.);
#24205=ORIENTED_EDGE('',*,*,#16688,.F.);
#24206=ORIENTED_EDGE('',*,*,#16689,.F.);
#24207=ORIENTED_EDGE('',*,*,#16690,.F.);
#24208=ORIENTED_EDGE('',*,*,#16683,.T.);
#24209=ORIENTED_EDGE('',*,*,#16691,.T.);
#24210=ORIENTED_EDGE('',*,*,#16692,.T.);
#24211=ORIENTED_EDGE('',*,*,#16693,.F.);
#24212=ORIENTED_EDGE('',*,*,#16694,.F.);
#24213=ORIENTED_EDGE('',*,*,#16695,.F.);
#24214=ORIENTED_EDGE('',*,*,#16688,.T.);
#24215=ORIENTED_EDGE('',*,*,#16696,.T.);
#24216=ORIENTED_EDGE('',*,*,#16697,.T.);
#24217=ORIENTED_EDGE('',*,*,#16698,.F.);
#24218=ORIENTED_EDGE('',*,*,#16699,.F.);
#24219=ORIENTED_EDGE('',*,*,#16700,.F.);
#24220=ORIENTED_EDGE('',*,*,#16693,.T.);
#24221=ORIENTED_EDGE('',*,*,#16701,.T.);
#24222=ORIENTED_EDGE('',*,*,#16702,.T.);
#24223=ORIENTED_EDGE('',*,*,#16703,.F.);
#24224=ORIENTED_EDGE('',*,*,#16704,.F.);
#24225=ORIENTED_EDGE('',*,*,#16705,.F.);
#24226=ORIENTED_EDGE('',*,*,#16698,.T.);
#24227=ORIENTED_EDGE('',*,*,#16706,.T.);
#24228=ORIENTED_EDGE('',*,*,#16707,.T.);
#24229=ORIENTED_EDGE('',*,*,#16708,.F.);
#24230=ORIENTED_EDGE('',*,*,#16709,.F.);
#24231=ORIENTED_EDGE('',*,*,#16710,.F.);
#24232=ORIENTED_EDGE('',*,*,#16703,.T.);
#24233=ORIENTED_EDGE('',*,*,#16711,.T.);
#24234=ORIENTED_EDGE('',*,*,#16712,.T.);
#24235=ORIENTED_EDGE('',*,*,#16713,.F.);
#24236=ORIENTED_EDGE('',*,*,#16714,.F.);
#24237=ORIENTED_EDGE('',*,*,#16715,.F.);
#24238=ORIENTED_EDGE('',*,*,#16708,.T.);
#24239=ORIENTED_EDGE('',*,*,#16716,.T.);
#24240=ORIENTED_EDGE('',*,*,#16717,.T.);
#24241=ORIENTED_EDGE('',*,*,#16718,.F.);
#24242=ORIENTED_EDGE('',*,*,#16719,.F.);
#24243=ORIENTED_EDGE('',*,*,#16720,.T.);
#24244=ORIENTED_EDGE('',*,*,#16721,.F.);
#24245=ORIENTED_EDGE('',*,*,#16722,.F.);
#24246=ORIENTED_EDGE('',*,*,#16718,.T.);
#24247=ORIENTED_EDGE('',*,*,#16723,.T.);
#24248=ORIENTED_EDGE('',*,*,#16724,.F.);
#24249=ORIENTED_EDGE('',*,*,#16725,.F.);
#24250=ORIENTED_EDGE('',*,*,#16726,.F.);
#24251=ORIENTED_EDGE('',*,*,#16721,.T.);
#24252=ORIENTED_EDGE('',*,*,#16727,.F.);
#24253=ORIENTED_EDGE('',*,*,#16728,.F.);
#24254=ORIENTED_EDGE('',*,*,#16729,.F.);
#24255=ORIENTED_EDGE('',*,*,#16725,.T.);
#24256=ORIENTED_EDGE('',*,*,#16730,.F.);
#24257=ORIENTED_EDGE('',*,*,#16731,.F.);
#24258=ORIENTED_EDGE('',*,*,#16732,.F.);
#24259=ORIENTED_EDGE('',*,*,#16733,.F.);
#24260=ORIENTED_EDGE('',*,*,#16734,.F.);
#24261=ORIENTED_EDGE('',*,*,#16735,.F.);
#24262=ORIENTED_EDGE('',*,*,#16736,.F.);
#24263=ORIENTED_EDGE('',*,*,#16731,.T.);
#24264=ORIENTED_EDGE('',*,*,#16737,.F.);
#24265=ORIENTED_EDGE('',*,*,#16738,.F.);
#24266=ORIENTED_EDGE('',*,*,#16739,.F.);
#24267=ORIENTED_EDGE('',*,*,#16735,.T.);
#24268=ORIENTED_EDGE('',*,*,#16740,.F.);
#24269=ORIENTED_EDGE('',*,*,#16741,.F.);
#24270=ORIENTED_EDGE('',*,*,#16742,.F.);
#24271=ORIENTED_EDGE('',*,*,#16743,.F.);
#24272=ORIENTED_EDGE('',*,*,#16738,.T.);
#24273=ORIENTED_EDGE('',*,*,#16744,.F.);
#24274=ORIENTED_EDGE('',*,*,#16745,.F.);
#24275=ORIENTED_EDGE('',*,*,#16746,.F.);
#24276=ORIENTED_EDGE('',*,*,#16747,.F.);
#24277=ORIENTED_EDGE('',*,*,#16748,.T.);
#24278=ORIENTED_EDGE('',*,*,#16749,.F.);
#24279=ORIENTED_EDGE('',*,*,#16750,.F.);
#24280=ORIENTED_EDGE('',*,*,#16751,.F.);
#24281=ORIENTED_EDGE('',*,*,#16752,.F.);
#24282=ORIENTED_EDGE('',*,*,#16753,.F.);
#24283=ORIENTED_EDGE('',*,*,#16745,.T.);
#24284=ORIENTED_EDGE('',*,*,#16754,.F.);
#24285=ORIENTED_EDGE('',*,*,#16755,.F.);
#24286=ORIENTED_EDGE('',*,*,#16756,.F.);
#24287=ORIENTED_EDGE('',*,*,#16751,.T.);
#24288=ORIENTED_EDGE('',*,*,#16757,.F.);
#24289=ORIENTED_EDGE('',*,*,#16758,.F.);
#24290=ORIENTED_EDGE('',*,*,#16759,.F.);
#24291=ORIENTED_EDGE('',*,*,#16760,.F.);
#24292=ORIENTED_EDGE('',*,*,#16761,.F.);
#24293=ORIENTED_EDGE('',*,*,#16755,.T.);
#24294=ORIENTED_EDGE('',*,*,#16762,.F.);
#24295=ORIENTED_EDGE('',*,*,#16763,.F.);
#24296=ORIENTED_EDGE('',*,*,#16764,.F.);
#24297=ORIENTED_EDGE('',*,*,#16765,.F.);
#24298=ORIENTED_EDGE('',*,*,#16759,.T.);
#24299=ORIENTED_EDGE('',*,*,#16766,.F.);
#24300=ORIENTED_EDGE('',*,*,#16767,.F.);
#24301=ORIENTED_EDGE('',*,*,#16768,.F.);
#24302=ORIENTED_EDGE('',*,*,#16769,.F.);
#24303=ORIENTED_EDGE('',*,*,#16764,.T.);
#24304=ORIENTED_EDGE('',*,*,#16770,.F.);
#24305=ORIENTED_EDGE('',*,*,#16771,.F.);
#24306=ORIENTED_EDGE('',*,*,#16772,.F.);
#24307=ORIENTED_EDGE('',*,*,#16773,.F.);
#24308=ORIENTED_EDGE('',*,*,#16767,.T.);
#24309=ORIENTED_EDGE('',*,*,#16774,.F.);
#24310=ORIENTED_EDGE('',*,*,#16775,.F.);
#24311=ORIENTED_EDGE('',*,*,#16776,.F.);
#24312=ORIENTED_EDGE('',*,*,#16777,.F.);
#24313=ORIENTED_EDGE('',*,*,#16772,.T.);
#24314=ORIENTED_EDGE('',*,*,#16778,.F.);
#24315=ORIENTED_EDGE('',*,*,#16779,.F.);
#24316=ORIENTED_EDGE('',*,*,#16780,.F.);
#24317=ORIENTED_EDGE('',*,*,#16781,.F.);
#24318=ORIENTED_EDGE('',*,*,#16775,.T.);
#24319=ORIENTED_EDGE('',*,*,#16782,.F.);
#24320=ORIENTED_EDGE('',*,*,#16783,.F.);
#24321=ORIENTED_EDGE('',*,*,#16784,.F.);
#24322=ORIENTED_EDGE('',*,*,#16785,.F.);
#24323=ORIENTED_EDGE('',*,*,#16786,.F.);
#24324=ORIENTED_EDGE('',*,*,#16780,.T.);
#24325=ORIENTED_EDGE('',*,*,#16787,.F.);
#24326=ORIENTED_EDGE('',*,*,#16788,.F.);
#24327=ORIENTED_EDGE('',*,*,#16789,.F.);
#24328=ORIENTED_EDGE('',*,*,#16790,.F.);
#24329=ORIENTED_EDGE('',*,*,#16784,.T.);
#24330=ORIENTED_EDGE('',*,*,#16791,.F.);
#24331=ORIENTED_EDGE('',*,*,#16792,.F.);
#24332=ORIENTED_EDGE('',*,*,#16793,.F.);
#24333=ORIENTED_EDGE('',*,*,#16794,.F.);
#24334=ORIENTED_EDGE('',*,*,#16789,.T.);
#24335=ORIENTED_EDGE('',*,*,#16795,.F.);
#24336=ORIENTED_EDGE('',*,*,#16796,.F.);
#24337=ORIENTED_EDGE('',*,*,#16797,.F.);
#24338=ORIENTED_EDGE('',*,*,#16798,.F.);
#24339=ORIENTED_EDGE('',*,*,#16799,.F.);
#24340=ORIENTED_EDGE('',*,*,#16792,.T.);
#24341=ORIENTED_EDGE('',*,*,#16800,.F.);
#24342=ORIENTED_EDGE('',*,*,#16801,.F.);
#24343=ORIENTED_EDGE('',*,*,#16802,.F.);
#24344=ORIENTED_EDGE('',*,*,#16803,.F.);
#24345=ORIENTED_EDGE('',*,*,#16797,.T.);
#24346=ORIENTED_EDGE('',*,*,#16804,.F.);
#24347=ORIENTED_EDGE('',*,*,#16805,.F.);
#24348=ORIENTED_EDGE('',*,*,#16806,.F.);
#24349=ORIENTED_EDGE('',*,*,#16807,.F.);
#24350=ORIENTED_EDGE('',*,*,#16801,.T.);
#24351=ORIENTED_EDGE('',*,*,#16808,.F.);
#24352=ORIENTED_EDGE('',*,*,#16809,.F.);
#24353=ORIENTED_EDGE('',*,*,#16810,.F.);
#24354=ORIENTED_EDGE('',*,*,#16811,.F.);
#24355=ORIENTED_EDGE('',*,*,#16812,.F.);
#24356=ORIENTED_EDGE('',*,*,#16806,.T.);
#24357=ORIENTED_EDGE('',*,*,#16813,.F.);
#24358=ORIENTED_EDGE('',*,*,#16814,.F.);
#24359=ORIENTED_EDGE('',*,*,#16815,.F.);
#24360=ORIENTED_EDGE('',*,*,#16816,.F.);
#24361=ORIENTED_EDGE('',*,*,#16810,.T.);
#24362=ORIENTED_EDGE('',*,*,#16817,.F.);
#24363=ORIENTED_EDGE('',*,*,#16818,.F.);
#24364=ORIENTED_EDGE('',*,*,#16819,.F.);
#24365=ORIENTED_EDGE('',*,*,#16820,.F.);
#24366=ORIENTED_EDGE('',*,*,#16815,.T.);
#24367=ORIENTED_EDGE('',*,*,#16821,.F.);
#24368=ORIENTED_EDGE('',*,*,#16822,.F.);
#24369=ORIENTED_EDGE('',*,*,#16823,.F.);
#24370=ORIENTED_EDGE('',*,*,#16824,.F.);
#24371=ORIENTED_EDGE('',*,*,#16825,.F.);
#24372=ORIENTED_EDGE('',*,*,#16818,.T.);
#24373=ORIENTED_EDGE('',*,*,#16826,.F.);
#24374=ORIENTED_EDGE('',*,*,#16827,.F.);
#24375=ORIENTED_EDGE('',*,*,#16828,.F.);
#24376=ORIENTED_EDGE('',*,*,#16829,.F.);
#24377=ORIENTED_EDGE('',*,*,#16823,.T.);
#24378=ORIENTED_EDGE('',*,*,#16830,.F.);
#24379=ORIENTED_EDGE('',*,*,#16831,.F.);
#24380=ORIENTED_EDGE('',*,*,#16832,.F.);
#24381=ORIENTED_EDGE('',*,*,#16833,.F.);
#24382=ORIENTED_EDGE('',*,*,#16827,.T.);
#24383=ORIENTED_EDGE('',*,*,#16834,.F.);
#24384=ORIENTED_EDGE('',*,*,#16835,.F.);
#24385=ORIENTED_EDGE('',*,*,#16836,.F.);
#24386=ORIENTED_EDGE('',*,*,#16837,.F.);
#24387=ORIENTED_EDGE('',*,*,#16832,.T.);
#24388=ORIENTED_EDGE('',*,*,#16838,.F.);
#24389=ORIENTED_EDGE('',*,*,#16839,.F.);
#24390=ORIENTED_EDGE('',*,*,#16840,.F.);
#24391=ORIENTED_EDGE('',*,*,#16841,.F.);
#24392=ORIENTED_EDGE('',*,*,#16835,.T.);
#24393=ORIENTED_EDGE('',*,*,#16842,.F.);
#24394=ORIENTED_EDGE('',*,*,#16843,.F.);
#24395=ORIENTED_EDGE('',*,*,#16844,.F.);
#24396=ORIENTED_EDGE('',*,*,#16845,.F.);
#24397=ORIENTED_EDGE('',*,*,#16840,.T.);
#24398=ORIENTED_EDGE('',*,*,#16846,.F.);
#24399=ORIENTED_EDGE('',*,*,#16847,.F.);
#24400=ORIENTED_EDGE('',*,*,#16848,.F.);
#24401=ORIENTED_EDGE('',*,*,#16849,.F.);
#24402=ORIENTED_EDGE('',*,*,#16850,.F.);
#24403=ORIENTED_EDGE('',*,*,#16843,.T.);
#24404=ORIENTED_EDGE('',*,*,#16851,.F.);
#24405=ORIENTED_EDGE('',*,*,#16852,.F.);
#24406=ORIENTED_EDGE('',*,*,#16853,.F.);
#24407=ORIENTED_EDGE('',*,*,#16848,.T.);
#24408=ORIENTED_EDGE('',*,*,#16854,.F.);
#24409=ORIENTED_EDGE('',*,*,#16855,.F.);
#24410=ORIENTED_EDGE('',*,*,#16856,.F.);
#24411=ORIENTED_EDGE('',*,*,#16857,.F.);
#24412=ORIENTED_EDGE('',*,*,#16858,.F.);
#24413=ORIENTED_EDGE('',*,*,#16852,.T.);
#24414=ORIENTED_EDGE('',*,*,#16859,.F.);
#24415=ORIENTED_EDGE('',*,*,#16860,.F.);
#24416=ORIENTED_EDGE('',*,*,#16861,.F.);
#24417=ORIENTED_EDGE('',*,*,#16862,.F.);
#24418=ORIENTED_EDGE('',*,*,#16863,.F.);
#24419=ORIENTED_EDGE('',*,*,#16864,.T.);
#24420=ORIENTED_EDGE('',*,*,#16865,.F.);
#24421=ORIENTED_EDGE('',*,*,#16866,.F.);
#24422=ORIENTED_EDGE('',*,*,#16867,.F.);
#24423=ORIENTED_EDGE('',*,*,#16868,.F.);
#24424=ORIENTED_EDGE('',*,*,#16869,.F.);
#24425=ORIENTED_EDGE('',*,*,#16861,.T.);
#24426=ORIENTED_EDGE('',*,*,#16870,.F.);
#24427=ORIENTED_EDGE('',*,*,#16871,.F.);
#24428=ORIENTED_EDGE('',*,*,#16872,.F.);
#24429=ORIENTED_EDGE('',*,*,#16867,.T.);
#24430=ORIENTED_EDGE('',*,*,#16873,.F.);
#24431=ORIENTED_EDGE('',*,*,#16874,.F.);
#24432=ORIENTED_EDGE('',*,*,#16875,.F.);
#24433=ORIENTED_EDGE('',*,*,#16876,.F.);
#24434=ORIENTED_EDGE('',*,*,#16877,.F.);
#24435=ORIENTED_EDGE('',*,*,#16871,.T.);
#24436=ORIENTED_EDGE('',*,*,#16878,.F.);
#24437=ORIENTED_EDGE('',*,*,#16879,.F.);
#24438=ORIENTED_EDGE('',*,*,#16880,.F.);
#24439=ORIENTED_EDGE('',*,*,#16881,.F.);
#24440=ORIENTED_EDGE('',*,*,#16875,.T.);
#24441=ORIENTED_EDGE('',*,*,#16882,.F.);
#24442=ORIENTED_EDGE('',*,*,#16883,.F.);
#24443=ORIENTED_EDGE('',*,*,#16884,.F.);
#24444=ORIENTED_EDGE('',*,*,#16885,.F.);
#24445=ORIENTED_EDGE('',*,*,#16880,.T.);
#24446=ORIENTED_EDGE('',*,*,#16886,.F.);
#24447=ORIENTED_EDGE('',*,*,#16887,.F.);
#24448=ORIENTED_EDGE('',*,*,#16888,.F.);
#24449=ORIENTED_EDGE('',*,*,#16889,.F.);
#24450=ORIENTED_EDGE('',*,*,#16883,.T.);
#24451=ORIENTED_EDGE('',*,*,#16890,.F.);
#24452=ORIENTED_EDGE('',*,*,#16891,.F.);
#24453=ORIENTED_EDGE('',*,*,#16892,.F.);
#24454=ORIENTED_EDGE('',*,*,#16893,.F.);
#24455=ORIENTED_EDGE('',*,*,#16888,.T.);
#24456=ORIENTED_EDGE('',*,*,#16894,.F.);
#24457=ORIENTED_EDGE('',*,*,#16895,.F.);
#24458=ORIENTED_EDGE('',*,*,#16896,.F.);
#24459=ORIENTED_EDGE('',*,*,#16897,.F.);
#24460=ORIENTED_EDGE('',*,*,#16891,.T.);
#24461=ORIENTED_EDGE('',*,*,#16898,.F.);
#24462=ORIENTED_EDGE('',*,*,#16899,.F.);
#24463=ORIENTED_EDGE('',*,*,#16900,.F.);
#24464=ORIENTED_EDGE('',*,*,#16901,.F.);
#24465=ORIENTED_EDGE('',*,*,#16902,.F.);
#24466=ORIENTED_EDGE('',*,*,#16896,.T.);
#24467=ORIENTED_EDGE('',*,*,#16903,.F.);
#24468=ORIENTED_EDGE('',*,*,#16904,.F.);
#24469=ORIENTED_EDGE('',*,*,#16905,.F.);
#24470=ORIENTED_EDGE('',*,*,#16906,.F.);
#24471=ORIENTED_EDGE('',*,*,#16900,.T.);
#24472=ORIENTED_EDGE('',*,*,#16907,.F.);
#24473=ORIENTED_EDGE('',*,*,#16908,.F.);
#24474=ORIENTED_EDGE('',*,*,#16909,.F.);
#24475=ORIENTED_EDGE('',*,*,#16910,.F.);
#24476=ORIENTED_EDGE('',*,*,#16905,.T.);
#24477=ORIENTED_EDGE('',*,*,#16911,.F.);
#24478=ORIENTED_EDGE('',*,*,#16912,.F.);
#24479=ORIENTED_EDGE('',*,*,#16913,.F.);
#24480=ORIENTED_EDGE('',*,*,#16914,.F.);
#24481=ORIENTED_EDGE('',*,*,#16915,.F.);
#24482=ORIENTED_EDGE('',*,*,#16908,.T.);
#24483=ORIENTED_EDGE('',*,*,#16916,.F.);
#24484=ORIENTED_EDGE('',*,*,#16917,.F.);
#24485=ORIENTED_EDGE('',*,*,#16918,.F.);
#24486=ORIENTED_EDGE('',*,*,#16919,.F.);
#24487=ORIENTED_EDGE('',*,*,#16913,.T.);
#24488=ORIENTED_EDGE('',*,*,#16920,.F.);
#24489=ORIENTED_EDGE('',*,*,#16921,.F.);
#24490=ORIENTED_EDGE('',*,*,#16922,.F.);
#24491=ORIENTED_EDGE('',*,*,#16923,.F.);
#24492=ORIENTED_EDGE('',*,*,#16917,.T.);
#24493=ORIENTED_EDGE('',*,*,#16924,.F.);
#24494=ORIENTED_EDGE('',*,*,#16925,.F.);
#24495=ORIENTED_EDGE('',*,*,#16926,.F.);
#24496=ORIENTED_EDGE('',*,*,#16927,.F.);
#24497=ORIENTED_EDGE('',*,*,#16928,.F.);
#24498=ORIENTED_EDGE('',*,*,#16922,.T.);
#24499=ORIENTED_EDGE('',*,*,#16929,.F.);
#24500=ORIENTED_EDGE('',*,*,#16930,.F.);
#24501=ORIENTED_EDGE('',*,*,#16931,.F.);
#24502=ORIENTED_EDGE('',*,*,#16932,.F.);
#24503=ORIENTED_EDGE('',*,*,#16926,.T.);
#24504=ORIENTED_EDGE('',*,*,#16933,.F.);
#24505=ORIENTED_EDGE('',*,*,#16934,.F.);
#24506=ORIENTED_EDGE('',*,*,#16935,.F.);
#24507=ORIENTED_EDGE('',*,*,#16936,.F.);
#24508=ORIENTED_EDGE('',*,*,#16931,.T.);
#24509=ORIENTED_EDGE('',*,*,#16937,.F.);
#24510=ORIENTED_EDGE('',*,*,#16938,.F.);
#24511=ORIENTED_EDGE('',*,*,#16939,.F.);
#24512=ORIENTED_EDGE('',*,*,#16940,.F.);
#24513=ORIENTED_EDGE('',*,*,#16941,.F.);
#24514=ORIENTED_EDGE('',*,*,#16934,.T.);
#24515=ORIENTED_EDGE('',*,*,#16942,.F.);
#24516=ORIENTED_EDGE('',*,*,#16943,.F.);
#24517=ORIENTED_EDGE('',*,*,#16944,.F.);
#24518=ORIENTED_EDGE('',*,*,#16945,.F.);
#24519=ORIENTED_EDGE('',*,*,#16939,.T.);
#24520=ORIENTED_EDGE('',*,*,#16946,.F.);
#24521=ORIENTED_EDGE('',*,*,#16947,.F.);
#24522=ORIENTED_EDGE('',*,*,#16948,.F.);
#24523=ORIENTED_EDGE('',*,*,#16949,.F.);
#24524=ORIENTED_EDGE('',*,*,#16943,.T.);
#24525=ORIENTED_EDGE('',*,*,#16950,.F.);
#24526=ORIENTED_EDGE('',*,*,#16951,.F.);
#24527=ORIENTED_EDGE('',*,*,#16952,.F.);
#24528=ORIENTED_EDGE('',*,*,#16953,.F.);
#24529=ORIENTED_EDGE('',*,*,#16948,.T.);
#24530=ORIENTED_EDGE('',*,*,#16954,.F.);
#24531=ORIENTED_EDGE('',*,*,#16955,.F.);
#24532=ORIENTED_EDGE('',*,*,#16956,.F.);
#24533=ORIENTED_EDGE('',*,*,#16957,.F.);
#24534=ORIENTED_EDGE('',*,*,#16951,.T.);
#24535=ORIENTED_EDGE('',*,*,#16958,.F.);
#24536=ORIENTED_EDGE('',*,*,#16959,.F.);
#24537=ORIENTED_EDGE('',*,*,#16960,.F.);
#24538=ORIENTED_EDGE('',*,*,#16961,.F.);
#24539=ORIENTED_EDGE('',*,*,#16956,.T.);
#24540=ORIENTED_EDGE('',*,*,#16962,.F.);
#24541=ORIENTED_EDGE('',*,*,#16963,.F.);
#24542=ORIENTED_EDGE('',*,*,#16964,.F.);
#24543=ORIENTED_EDGE('',*,*,#16965,.F.);
#24544=ORIENTED_EDGE('',*,*,#16966,.F.);
#24545=ORIENTED_EDGE('',*,*,#16959,.T.);
#24546=ORIENTED_EDGE('',*,*,#16967,.F.);
#24547=ORIENTED_EDGE('',*,*,#16968,.F.);
#24548=ORIENTED_EDGE('',*,*,#16969,.F.);
#24549=ORIENTED_EDGE('',*,*,#16964,.T.);
#24550=ORIENTED_EDGE('',*,*,#16970,.F.);
#24551=ORIENTED_EDGE('',*,*,#16971,.F.);
#24552=ORIENTED_EDGE('',*,*,#16972,.F.);
#24553=ORIENTED_EDGE('',*,*,#16973,.F.);
#24554=ORIENTED_EDGE('',*,*,#16974,.F.);
#24555=ORIENTED_EDGE('',*,*,#16968,.T.);
#24556=ORIENTED_EDGE('',*,*,#16975,.F.);
#24557=ORIENTED_EDGE('',*,*,#16976,.F.);
#24558=ORIENTED_EDGE('',*,*,#16977,.F.);
#24559=ORIENTED_EDGE('',*,*,#16978,.F.);
#24560=ORIENTED_EDGE('',*,*,#16979,.F.);
#24561=ORIENTED_EDGE('',*,*,#16980,.T.);
#24562=ORIENTED_EDGE('',*,*,#16981,.F.);
#24563=ORIENTED_EDGE('',*,*,#16982,.F.);
#24564=ORIENTED_EDGE('',*,*,#16983,.F.);
#24565=ORIENTED_EDGE('',*,*,#16984,.F.);
#24566=ORIENTED_EDGE('',*,*,#16985,.F.);
#24567=ORIENTED_EDGE('',*,*,#16977,.T.);
#24568=ORIENTED_EDGE('',*,*,#16986,.F.);
#24569=ORIENTED_EDGE('',*,*,#16987,.F.);
#24570=ORIENTED_EDGE('',*,*,#16988,.F.);
#24571=ORIENTED_EDGE('',*,*,#16983,.T.);
#24572=ORIENTED_EDGE('',*,*,#16989,.F.);
#24573=ORIENTED_EDGE('',*,*,#16990,.F.);
#24574=ORIENTED_EDGE('',*,*,#16991,.F.);
#24575=ORIENTED_EDGE('',*,*,#16992,.F.);
#24576=ORIENTED_EDGE('',*,*,#16993,.F.);
#24577=ORIENTED_EDGE('',*,*,#16987,.T.);
#24578=ORIENTED_EDGE('',*,*,#16994,.F.);
#24579=ORIENTED_EDGE('',*,*,#16995,.F.);
#24580=ORIENTED_EDGE('',*,*,#16996,.F.);
#24581=ORIENTED_EDGE('',*,*,#16997,.F.);
#24582=ORIENTED_EDGE('',*,*,#16991,.T.);
#24583=ORIENTED_EDGE('',*,*,#16998,.F.);
#24584=ORIENTED_EDGE('',*,*,#16999,.F.);
#24585=ORIENTED_EDGE('',*,*,#17000,.F.);
#24586=ORIENTED_EDGE('',*,*,#17001,.F.);
#24587=ORIENTED_EDGE('',*,*,#16996,.T.);
#24588=ORIENTED_EDGE('',*,*,#17002,.F.);
#24589=ORIENTED_EDGE('',*,*,#17003,.F.);
#24590=ORIENTED_EDGE('',*,*,#17004,.F.);
#24591=ORIENTED_EDGE('',*,*,#17005,.F.);
#24592=ORIENTED_EDGE('',*,*,#16999,.T.);
#24593=ORIENTED_EDGE('',*,*,#17006,.F.);
#24594=ORIENTED_EDGE('',*,*,#17007,.F.);
#24595=ORIENTED_EDGE('',*,*,#17008,.F.);
#24596=ORIENTED_EDGE('',*,*,#17009,.F.);
#24597=ORIENTED_EDGE('',*,*,#17004,.T.);
#24598=ORIENTED_EDGE('',*,*,#17010,.F.);
#24599=ORIENTED_EDGE('',*,*,#17011,.F.);
#24600=ORIENTED_EDGE('',*,*,#17012,.F.);
#24601=ORIENTED_EDGE('',*,*,#17013,.F.);
#24602=ORIENTED_EDGE('',*,*,#17007,.T.);
#24603=ORIENTED_EDGE('',*,*,#17014,.F.);
#24604=ORIENTED_EDGE('',*,*,#17015,.F.);
#24605=ORIENTED_EDGE('',*,*,#17016,.F.);
#24606=ORIENTED_EDGE('',*,*,#17017,.F.);
#24607=ORIENTED_EDGE('',*,*,#17018,.F.);
#24608=ORIENTED_EDGE('',*,*,#17012,.T.);
#24609=ORIENTED_EDGE('',*,*,#17019,.F.);
#24610=ORIENTED_EDGE('',*,*,#17020,.F.);
#24611=ORIENTED_EDGE('',*,*,#17021,.F.);
#24612=ORIENTED_EDGE('',*,*,#17022,.F.);
#24613=ORIENTED_EDGE('',*,*,#17016,.T.);
#24614=ORIENTED_EDGE('',*,*,#17023,.F.);
#24615=ORIENTED_EDGE('',*,*,#17024,.F.);
#24616=ORIENTED_EDGE('',*,*,#17025,.F.);
#24617=ORIENTED_EDGE('',*,*,#17026,.F.);
#24618=ORIENTED_EDGE('',*,*,#17021,.T.);
#24619=ORIENTED_EDGE('',*,*,#17027,.F.);
#24620=ORIENTED_EDGE('',*,*,#17028,.F.);
#24621=ORIENTED_EDGE('',*,*,#17029,.F.);
#24622=ORIENTED_EDGE('',*,*,#17030,.F.);
#24623=ORIENTED_EDGE('',*,*,#17031,.F.);
#24624=ORIENTED_EDGE('',*,*,#17024,.T.);
#24625=ORIENTED_EDGE('',*,*,#17032,.F.);
#24626=ORIENTED_EDGE('',*,*,#17033,.F.);
#24627=ORIENTED_EDGE('',*,*,#17034,.F.);
#24628=ORIENTED_EDGE('',*,*,#17035,.F.);
#24629=ORIENTED_EDGE('',*,*,#17029,.T.);
#24630=ORIENTED_EDGE('',*,*,#17036,.F.);
#24631=ORIENTED_EDGE('',*,*,#17037,.F.);
#24632=ORIENTED_EDGE('',*,*,#17038,.F.);
#24633=ORIENTED_EDGE('',*,*,#17039,.F.);
#24634=ORIENTED_EDGE('',*,*,#17033,.T.);
#24635=ORIENTED_EDGE('',*,*,#17040,.F.);
#24636=ORIENTED_EDGE('',*,*,#17041,.F.);
#24637=ORIENTED_EDGE('',*,*,#17042,.F.);
#24638=ORIENTED_EDGE('',*,*,#17043,.F.);
#24639=ORIENTED_EDGE('',*,*,#17044,.F.);
#24640=ORIENTED_EDGE('',*,*,#17038,.T.);
#24641=ORIENTED_EDGE('',*,*,#17045,.F.);
#24642=ORIENTED_EDGE('',*,*,#17046,.F.);
#24643=ORIENTED_EDGE('',*,*,#17047,.F.);
#24644=ORIENTED_EDGE('',*,*,#17048,.F.);
#24645=ORIENTED_EDGE('',*,*,#17042,.T.);
#24646=ORIENTED_EDGE('',*,*,#17049,.F.);
#24647=ORIENTED_EDGE('',*,*,#17050,.F.);
#24648=ORIENTED_EDGE('',*,*,#17051,.F.);
#24649=ORIENTED_EDGE('',*,*,#17052,.F.);
#24650=ORIENTED_EDGE('',*,*,#17047,.T.);
#24651=ORIENTED_EDGE('',*,*,#17053,.F.);
#24652=ORIENTED_EDGE('',*,*,#17054,.F.);
#24653=ORIENTED_EDGE('',*,*,#17055,.F.);
#24654=ORIENTED_EDGE('',*,*,#17056,.F.);
#24655=ORIENTED_EDGE('',*,*,#17057,.F.);
#24656=ORIENTED_EDGE('',*,*,#17050,.T.);
#24657=ORIENTED_EDGE('',*,*,#17058,.F.);
#24658=ORIENTED_EDGE('',*,*,#17059,.F.);
#24659=ORIENTED_EDGE('',*,*,#17060,.F.);
#24660=ORIENTED_EDGE('',*,*,#17061,.F.);
#24661=ORIENTED_EDGE('',*,*,#17055,.T.);
#24662=ORIENTED_EDGE('',*,*,#17062,.F.);
#24663=ORIENTED_EDGE('',*,*,#17063,.F.);
#24664=ORIENTED_EDGE('',*,*,#17064,.F.);
#24665=ORIENTED_EDGE('',*,*,#17065,.F.);
#24666=ORIENTED_EDGE('',*,*,#17059,.T.);
#24667=ORIENTED_EDGE('',*,*,#17066,.F.);
#24668=ORIENTED_EDGE('',*,*,#17067,.F.);
#24669=ORIENTED_EDGE('',*,*,#17068,.F.);
#24670=ORIENTED_EDGE('',*,*,#17069,.F.);
#24671=ORIENTED_EDGE('',*,*,#17064,.T.);
#24672=ORIENTED_EDGE('',*,*,#17070,.F.);
#24673=ORIENTED_EDGE('',*,*,#17071,.F.);
#24674=ORIENTED_EDGE('',*,*,#17072,.F.);
#24675=ORIENTED_EDGE('',*,*,#17073,.F.);
#24676=ORIENTED_EDGE('',*,*,#17067,.T.);
#24677=ORIENTED_EDGE('',*,*,#17074,.F.);
#24678=ORIENTED_EDGE('',*,*,#17075,.F.);
#24679=ORIENTED_EDGE('',*,*,#17076,.F.);
#24680=ORIENTED_EDGE('',*,*,#17077,.F.);
#24681=ORIENTED_EDGE('',*,*,#17072,.T.);
#24682=ORIENTED_EDGE('',*,*,#17078,.F.);
#24683=ORIENTED_EDGE('',*,*,#17079,.F.);
#24684=ORIENTED_EDGE('',*,*,#17080,.F.);
#24685=ORIENTED_EDGE('',*,*,#17081,.F.);
#24686=ORIENTED_EDGE('',*,*,#17082,.F.);
#24687=ORIENTED_EDGE('',*,*,#17075,.T.);
#24688=ORIENTED_EDGE('',*,*,#17083,.F.);
#24689=ORIENTED_EDGE('',*,*,#17084,.F.);
#24690=ORIENTED_EDGE('',*,*,#17085,.F.);
#24691=ORIENTED_EDGE('',*,*,#17080,.T.);
#24692=ORIENTED_EDGE('',*,*,#17086,.F.);
#24693=ORIENTED_EDGE('',*,*,#17087,.F.);
#24694=ORIENTED_EDGE('',*,*,#17088,.F.);
#24695=ORIENTED_EDGE('',*,*,#17089,.F.);
#24696=ORIENTED_EDGE('',*,*,#17090,.F.);
#24697=ORIENTED_EDGE('',*,*,#17084,.T.);
#24698=ORIENTED_EDGE('',*,*,#17091,.F.);
#24699=ORIENTED_EDGE('',*,*,#17092,.F.);
#24700=ORIENTED_EDGE('',*,*,#17093,.F.);
#24701=ORIENTED_EDGE('',*,*,#17094,.F.);
#24702=ORIENTED_EDGE('',*,*,#17095,.F.);
#24703=ORIENTED_EDGE('',*,*,#17096,.T.);
#24704=ORIENTED_EDGE('',*,*,#17097,.F.);
#24705=ORIENTED_EDGE('',*,*,#17098,.F.);
#24706=ORIENTED_EDGE('',*,*,#17099,.F.);
#24707=ORIENTED_EDGE('',*,*,#17100,.F.);
#24708=ORIENTED_EDGE('',*,*,#17101,.F.);
#24709=ORIENTED_EDGE('',*,*,#17093,.T.);
#24710=ORIENTED_EDGE('',*,*,#17102,.F.);
#24711=ORIENTED_EDGE('',*,*,#17103,.F.);
#24712=ORIENTED_EDGE('',*,*,#17104,.F.);
#24713=ORIENTED_EDGE('',*,*,#17099,.T.);
#24714=ORIENTED_EDGE('',*,*,#17105,.F.);
#24715=ORIENTED_EDGE('',*,*,#17106,.F.);
#24716=ORIENTED_EDGE('',*,*,#17107,.F.);
#24717=ORIENTED_EDGE('',*,*,#17108,.F.);
#24718=ORIENTED_EDGE('',*,*,#17109,.F.);
#24719=ORIENTED_EDGE('',*,*,#17103,.T.);
#24720=ORIENTED_EDGE('',*,*,#17110,.F.);
#24721=ORIENTED_EDGE('',*,*,#17111,.F.);
#24722=ORIENTED_EDGE('',*,*,#17112,.F.);
#24723=ORIENTED_EDGE('',*,*,#17113,.F.);
#24724=ORIENTED_EDGE('',*,*,#17107,.T.);
#24725=ORIENTED_EDGE('',*,*,#17114,.F.);
#24726=ORIENTED_EDGE('',*,*,#17115,.F.);
#24727=ORIENTED_EDGE('',*,*,#17116,.F.);
#24728=ORIENTED_EDGE('',*,*,#17117,.F.);
#24729=ORIENTED_EDGE('',*,*,#17112,.T.);
#24730=ORIENTED_EDGE('',*,*,#17118,.F.);
#24731=ORIENTED_EDGE('',*,*,#17119,.F.);
#24732=ORIENTED_EDGE('',*,*,#17120,.F.);
#24733=ORIENTED_EDGE('',*,*,#17121,.F.);
#24734=ORIENTED_EDGE('',*,*,#17115,.T.);
#24735=ORIENTED_EDGE('',*,*,#17122,.F.);
#24736=ORIENTED_EDGE('',*,*,#17123,.F.);
#24737=ORIENTED_EDGE('',*,*,#17124,.F.);
#24738=ORIENTED_EDGE('',*,*,#17125,.F.);
#24739=ORIENTED_EDGE('',*,*,#17120,.T.);
#24740=ORIENTED_EDGE('',*,*,#17126,.F.);
#24741=ORIENTED_EDGE('',*,*,#17127,.F.);
#24742=ORIENTED_EDGE('',*,*,#17128,.F.);
#24743=ORIENTED_EDGE('',*,*,#17129,.F.);
#24744=ORIENTED_EDGE('',*,*,#17123,.T.);
#24745=ORIENTED_EDGE('',*,*,#17130,.F.);
#24746=ORIENTED_EDGE('',*,*,#17131,.F.);
#24747=ORIENTED_EDGE('',*,*,#17132,.F.);
#24748=ORIENTED_EDGE('',*,*,#17133,.F.);
#24749=ORIENTED_EDGE('',*,*,#17134,.F.);
#24750=ORIENTED_EDGE('',*,*,#17128,.T.);
#24751=ORIENTED_EDGE('',*,*,#17135,.F.);
#24752=ORIENTED_EDGE('',*,*,#17136,.F.);
#24753=ORIENTED_EDGE('',*,*,#17137,.F.);
#24754=ORIENTED_EDGE('',*,*,#17138,.F.);
#24755=ORIENTED_EDGE('',*,*,#17132,.T.);
#24756=ORIENTED_EDGE('',*,*,#17139,.F.);
#24757=ORIENTED_EDGE('',*,*,#17140,.F.);
#24758=ORIENTED_EDGE('',*,*,#17141,.F.);
#24759=ORIENTED_EDGE('',*,*,#17142,.F.);
#24760=ORIENTED_EDGE('',*,*,#17137,.T.);
#24761=ORIENTED_EDGE('',*,*,#17143,.F.);
#24762=ORIENTED_EDGE('',*,*,#17144,.F.);
#24763=ORIENTED_EDGE('',*,*,#17145,.F.);
#24764=ORIENTED_EDGE('',*,*,#17146,.F.);
#24765=ORIENTED_EDGE('',*,*,#17147,.F.);
#24766=ORIENTED_EDGE('',*,*,#17140,.T.);
#24767=ORIENTED_EDGE('',*,*,#17148,.F.);
#24768=ORIENTED_EDGE('',*,*,#17149,.F.);
#24769=ORIENTED_EDGE('',*,*,#17150,.F.);
#24770=ORIENTED_EDGE('',*,*,#17151,.F.);
#24771=ORIENTED_EDGE('',*,*,#17145,.T.);
#24772=ORIENTED_EDGE('',*,*,#17152,.F.);
#24773=ORIENTED_EDGE('',*,*,#17153,.F.);
#24774=ORIENTED_EDGE('',*,*,#17154,.F.);
#24775=ORIENTED_EDGE('',*,*,#17155,.F.);
#24776=ORIENTED_EDGE('',*,*,#17149,.T.);
#24777=ORIENTED_EDGE('',*,*,#17156,.F.);
#24778=ORIENTED_EDGE('',*,*,#17157,.F.);
#24779=ORIENTED_EDGE('',*,*,#17158,.F.);
#24780=ORIENTED_EDGE('',*,*,#17159,.F.);
#24781=ORIENTED_EDGE('',*,*,#17160,.F.);
#24782=ORIENTED_EDGE('',*,*,#17154,.T.);
#24783=ORIENTED_EDGE('',*,*,#17161,.F.);
#24784=ORIENTED_EDGE('',*,*,#17162,.F.);
#24785=ORIENTED_EDGE('',*,*,#17163,.F.);
#24786=ORIENTED_EDGE('',*,*,#17164,.F.);
#24787=ORIENTED_EDGE('',*,*,#17158,.T.);
#24788=ORIENTED_EDGE('',*,*,#17165,.F.);
#24789=ORIENTED_EDGE('',*,*,#17166,.F.);
#24790=ORIENTED_EDGE('',*,*,#17167,.F.);
#24791=ORIENTED_EDGE('',*,*,#17168,.F.);
#24792=ORIENTED_EDGE('',*,*,#17163,.T.);
#24793=ORIENTED_EDGE('',*,*,#17169,.F.);
#24794=ORIENTED_EDGE('',*,*,#17170,.F.);
#24795=ORIENTED_EDGE('',*,*,#17171,.F.);
#24796=ORIENTED_EDGE('',*,*,#17172,.F.);
#24797=ORIENTED_EDGE('',*,*,#17173,.F.);
#24798=ORIENTED_EDGE('',*,*,#17166,.T.);
#24799=ORIENTED_EDGE('',*,*,#17174,.F.);
#24800=ORIENTED_EDGE('',*,*,#17175,.F.);
#24801=ORIENTED_EDGE('',*,*,#17176,.F.);
#24802=ORIENTED_EDGE('',*,*,#17177,.F.);
#24803=ORIENTED_EDGE('',*,*,#17171,.T.);
#24804=ORIENTED_EDGE('',*,*,#17178,.F.);
#24805=ORIENTED_EDGE('',*,*,#17179,.F.);
#24806=ORIENTED_EDGE('',*,*,#17180,.F.);
#24807=ORIENTED_EDGE('',*,*,#17181,.F.);
#24808=ORIENTED_EDGE('',*,*,#17175,.T.);
#24809=ORIENTED_EDGE('',*,*,#17182,.F.);
#24810=ORIENTED_EDGE('',*,*,#17183,.F.);
#24811=ORIENTED_EDGE('',*,*,#17184,.F.);
#24812=ORIENTED_EDGE('',*,*,#17185,.F.);
#24813=ORIENTED_EDGE('',*,*,#17180,.T.);
#24814=ORIENTED_EDGE('',*,*,#17186,.F.);
#24815=ORIENTED_EDGE('',*,*,#17187,.F.);
#24816=ORIENTED_EDGE('',*,*,#17188,.F.);
#24817=ORIENTED_EDGE('',*,*,#17189,.F.);
#24818=ORIENTED_EDGE('',*,*,#17183,.T.);
#24819=ORIENTED_EDGE('',*,*,#17190,.F.);
#24820=ORIENTED_EDGE('',*,*,#17191,.F.);
#24821=ORIENTED_EDGE('',*,*,#17192,.F.);
#24822=ORIENTED_EDGE('',*,*,#17193,.F.);
#24823=ORIENTED_EDGE('',*,*,#17188,.T.);
#24824=ORIENTED_EDGE('',*,*,#17194,.F.);
#24825=ORIENTED_EDGE('',*,*,#17195,.F.);
#24826=ORIENTED_EDGE('',*,*,#17196,.F.);
#24827=ORIENTED_EDGE('',*,*,#17197,.F.);
#24828=ORIENTED_EDGE('',*,*,#17198,.F.);
#24829=ORIENTED_EDGE('',*,*,#17191,.T.);
#24830=ORIENTED_EDGE('',*,*,#17199,.F.);
#24831=ORIENTED_EDGE('',*,*,#17200,.F.);
#24832=ORIENTED_EDGE('',*,*,#17201,.F.);
#24833=ORIENTED_EDGE('',*,*,#17196,.T.);
#24834=ORIENTED_EDGE('',*,*,#17202,.F.);
#24835=ORIENTED_EDGE('',*,*,#17203,.F.);
#24836=ORIENTED_EDGE('',*,*,#17204,.F.);
#24837=ORIENTED_EDGE('',*,*,#17205,.F.);
#24838=ORIENTED_EDGE('',*,*,#17206,.F.);
#24839=ORIENTED_EDGE('',*,*,#17200,.T.);
#24840=ORIENTED_EDGE('',*,*,#17207,.F.);
#24841=ORIENTED_EDGE('',*,*,#17208,.F.);
#24842=ORIENTED_EDGE('',*,*,#17204,.T.);
#24843=ORIENTED_EDGE('',*,*,#17209,.F.);
#24844=ORIENTED_EDGE('',*,*,#17210,.T.);
#24845=ORIENTED_EDGE('',*,*,#17211,.F.);
#24846=ORIENTED_EDGE('',*,*,#17088,.T.);
#24847=ORIENTED_EDGE('',*,*,#17212,.F.);
#24848=ORIENTED_EDGE('',*,*,#17213,.T.);
#24849=ORIENTED_EDGE('',*,*,#17214,.F.);
#24850=ORIENTED_EDGE('',*,*,#16972,.T.);
#24851=ORIENTED_EDGE('',*,*,#17215,.F.);
#24852=ORIENTED_EDGE('',*,*,#17216,.T.);
#24853=ORIENTED_EDGE('',*,*,#17217,.F.);
#24854=ORIENTED_EDGE('',*,*,#16856,.T.);
#24855=ORIENTED_EDGE('',*,*,#17218,.F.);
#24856=ORIENTED_EDGE('',*,*,#17219,.T.);
#24857=ORIENTED_EDGE('',*,*,#17220,.F.);
#24858=ORIENTED_EDGE('',*,*,#16741,.T.);
#24859=ORIENTED_EDGE('',*,*,#17221,.F.);
#24860=ORIENTED_EDGE('',*,*,#17222,.F.);
#24861=ORIENTED_EDGE('',*,*,#16728,.T.);
#24862=ORIENTED_EDGE('',*,*,#17223,.F.);
#24863=ORIENTED_EDGE('',*,*,#17224,.F.);
#24864=ORIENTED_EDGE('',*,*,#17225,.F.);
#24865=ORIENTED_EDGE('',*,*,#16713,.T.);
#24866=ORIENTED_EDGE('',*,*,#17226,.T.);
#24867=ORIENTED_EDGE('',*,*,#17227,.T.);
#24868=ORIENTED_EDGE('',*,*,#17228,.T.);
#24869=ORIENTED_EDGE('',*,*,#17229,.F.);
#24870=ORIENTED_EDGE('',*,*,#17230,.F.);
#24871=ORIENTED_EDGE('',*,*,#16577,.T.);
#24872=ORIENTED_EDGE('',*,*,#17231,.T.);
#24873=ORIENTED_EDGE('',*,*,#17232,.T.);
#24874=ORIENTED_EDGE('',*,*,#17233,.T.);
#24875=ORIENTED_EDGE('',*,*,#17234,.F.);
#24876=ORIENTED_EDGE('',*,*,#17235,.F.);
#24877=ORIENTED_EDGE('',*,*,#16441,.T.);
#24878=ORIENTED_EDGE('',*,*,#17236,.T.);
#24879=ORIENTED_EDGE('',*,*,#17237,.T.);
#24880=ORIENTED_EDGE('',*,*,#17238,.T.);
#24881=ORIENTED_EDGE('',*,*,#17239,.F.);
#24882=ORIENTED_EDGE('',*,*,#17240,.F.);
#24883=ORIENTED_EDGE('',*,*,#16305,.T.);
#24884=ORIENTED_EDGE('',*,*,#17241,.T.);
#24885=ORIENTED_EDGE('',*,*,#17242,.T.);
#24886=ORIENTED_EDGE('',*,*,#17243,.T.);
#24887=ORIENTED_EDGE('',*,*,#17244,.F.);
#24888=ORIENTED_EDGE('',*,*,#17245,.F.);
#24889=ORIENTED_EDGE('',*,*,#16169,.T.);
#24890=ORIENTED_EDGE('',*,*,#17246,.T.);
#24891=ORIENTED_EDGE('',*,*,#17247,.T.);
#24892=ORIENTED_EDGE('',*,*,#17248,.T.);
#24893=ORIENTED_EDGE('',*,*,#17249,.F.);
#24894=ORIENTED_EDGE('',*,*,#17250,.F.);
#24895=ORIENTED_EDGE('',*,*,#16150,.T.);
#24896=ORIENTED_EDGE('',*,*,#17251,.T.);
#24897=ORIENTED_EDGE('',*,*,#17252,.T.);
#24898=ORIENTED_EDGE('',*,*,#17253,.T.);
#24899=ORIENTED_EDGE('',*,*,#17254,.F.);
#24900=ORIENTED_EDGE('',*,*,#17255,.F.);
#24901=ORIENTED_EDGE('',*,*,#17256,.F.);
#24902=ORIENTED_EDGE('',*,*,#17257,.T.);
#24903=ORIENTED_EDGE('',*,*,#17258,.T.);
#24904=ORIENTED_EDGE('',*,*,#17257,.F.);
#24905=ORIENTED_EDGE('',*,*,#17256,.T.);
#24906=ORIENTED_EDGE('',*,*,#17259,.T.);
#24907=ORIENTED_EDGE('',*,*,#17260,.T.);
#24908=ORIENTED_EDGE('',*,*,#17261,.F.);
#24909=ORIENTED_EDGE('',*,*,#17262,.T.);
#24910=ORIENTED_EDGE('',*,*,#17263,.T.);
#24911=ORIENTED_EDGE('',*,*,#17264,.T.);
#24912=ORIENTED_EDGE('',*,*,#17265,.T.);
#24913=ORIENTED_EDGE('',*,*,#17266,.T.);
#24914=ORIENTED_EDGE('',*,*,#17261,.T.);
#24915=ORIENTED_EDGE('',*,*,#17267,.F.);
#24916=ORIENTED_EDGE('',*,*,#17268,.T.);
#24917=ORIENTED_EDGE('',*,*,#17269,.T.);
#24918=ORIENTED_EDGE('',*,*,#17268,.F.);
#24919=ORIENTED_EDGE('',*,*,#17267,.T.);
#24920=ORIENTED_EDGE('',*,*,#17270,.T.);
#24921=ORIENTED_EDGE('',*,*,#17271,.T.);
#24922=ORIENTED_EDGE('',*,*,#17272,.F.);
#24923=ORIENTED_EDGE('',*,*,#17273,.T.);
#24924=ORIENTED_EDGE('',*,*,#17274,.T.);
#24925=ORIENTED_EDGE('',*,*,#17275,.T.);
#24926=ORIENTED_EDGE('',*,*,#17276,.T.);
#24927=ORIENTED_EDGE('',*,*,#17272,.T.);
#24928=ORIENTED_EDGE('',*,*,#17277,.T.);
#24929=ORIENTED_EDGE('',*,*,#17278,.F.);
#24930=ORIENTED_EDGE('',*,*,#17279,.T.);
#24931=ORIENTED_EDGE('',*,*,#17280,.T.);
#24932=ORIENTED_EDGE('',*,*,#17279,.F.);
#24933=ORIENTED_EDGE('',*,*,#17278,.T.);
#24934=ORIENTED_EDGE('',*,*,#17265,.F.);
#24935=ORIENTED_EDGE('',*,*,#17281,.F.);
#24936=ORIENTED_EDGE('',*,*,#17282,.F.);
#24937=ORIENTED_EDGE('',*,*,#17283,.T.);
#24938=ORIENTED_EDGE('',*,*,#17276,.F.);
#24939=ORIENTED_EDGE('',*,*,#17284,.F.);
#24940=ORIENTED_EDGE('',*,*,#17285,.T.);
#24941=ORIENTED_EDGE('',*,*,#17286,.T.);
#24942=ORIENTED_EDGE('',*,*,#17287,.T.);
#24943=ORIENTED_EDGE('',*,*,#17273,.F.);
#24944=ORIENTED_EDGE('',*,*,#17266,.F.);
#24945=ORIENTED_EDGE('',*,*,#17283,.F.);
#24946=ORIENTED_EDGE('',*,*,#17288,.T.);
#24947=ORIENTED_EDGE('',*,*,#17289,.T.);
#24948=ORIENTED_EDGE('',*,*,#17277,.F.);
#24949=ORIENTED_EDGE('',*,*,#17271,.F.);
#24950=ORIENTED_EDGE('',*,*,#17290,.T.);
#24951=ORIENTED_EDGE('',*,*,#17262,.F.);
#24952=ORIENTED_EDGE('',*,*,#17259,.F.);
#24953=ORIENTED_EDGE('',*,*,#17290,.F.);
#24954=ORIENTED_EDGE('',*,*,#17270,.F.);
#24955=ORIENTED_EDGE('',*,*,#17287,.F.);
#24956=ORIENTED_EDGE('',*,*,#17291,.F.);
#24957=ORIENTED_EDGE('',*,*,#17292,.F.);
#24958=ORIENTED_EDGE('',*,*,#17293,.F.);
#24959=ORIENTED_EDGE('',*,*,#17294,.F.);
#24960=ORIENTED_EDGE('',*,*,#17295,.F.);
#24961=ORIENTED_EDGE('',*,*,#17296,.F.);
#24962=ORIENTED_EDGE('',*,*,#17297,.F.);
#24963=ORIENTED_EDGE('',*,*,#17298,.F.);
#24964=ORIENTED_EDGE('',*,*,#17299,.F.);
#24965=ORIENTED_EDGE('',*,*,#17300,.F.);
#24966=ORIENTED_EDGE('',*,*,#17301,.F.);
#24967=ORIENTED_EDGE('',*,*,#17302,.F.);
#24968=ORIENTED_EDGE('',*,*,#17303,.F.);
#24969=ORIENTED_EDGE('',*,*,#17304,.F.);
#24970=ORIENTED_EDGE('',*,*,#17305,.F.);
#24971=ORIENTED_EDGE('',*,*,#17306,.F.);
#24972=ORIENTED_EDGE('',*,*,#17307,.F.);
#24973=ORIENTED_EDGE('',*,*,#17308,.F.);
#24974=ORIENTED_EDGE('',*,*,#17309,.F.);
#24975=ORIENTED_EDGE('',*,*,#17310,.F.);
#24976=ORIENTED_EDGE('',*,*,#17311,.F.);
#24977=ORIENTED_EDGE('',*,*,#17312,.F.);
#24978=ORIENTED_EDGE('',*,*,#17313,.F.);
#24979=ORIENTED_EDGE('',*,*,#17314,.F.);
#24980=ORIENTED_EDGE('',*,*,#17315,.F.);
#24981=ORIENTED_EDGE('',*,*,#17316,.F.);
#24982=ORIENTED_EDGE('',*,*,#17317,.F.);
#24983=ORIENTED_EDGE('',*,*,#17318,.F.);
#24984=ORIENTED_EDGE('',*,*,#17319,.F.);
#24985=ORIENTED_EDGE('',*,*,#17320,.F.);
#24986=ORIENTED_EDGE('',*,*,#17321,.F.);
#24987=ORIENTED_EDGE('',*,*,#17210,.F.);
#24988=ORIENTED_EDGE('',*,*,#17322,.F.);
#24989=ORIENTED_EDGE('',*,*,#17243,.F.);
#24990=ORIENTED_EDGE('',*,*,#17323,.F.);
#24991=ORIENTED_EDGE('',*,*,#17213,.F.);
#24992=ORIENTED_EDGE('',*,*,#17324,.F.);
#24993=ORIENTED_EDGE('',*,*,#17238,.F.);
#24994=ORIENTED_EDGE('',*,*,#17325,.F.);
#24995=ORIENTED_EDGE('',*,*,#17216,.F.);
#24996=ORIENTED_EDGE('',*,*,#17326,.F.);
#24997=ORIENTED_EDGE('',*,*,#17233,.F.);
#24998=ORIENTED_EDGE('',*,*,#17327,.F.);
#24999=ORIENTED_EDGE('',*,*,#17219,.F.);
#25000=ORIENTED_EDGE('',*,*,#17328,.F.);
#25001=ORIENTED_EDGE('',*,*,#17228,.F.);
#25002=ORIENTED_EDGE('',*,*,#17280,.F.);
#25003=ORIENTED_EDGE('',*,*,#17269,.F.);
#25004=ORIENTED_EDGE('',*,*,#17258,.F.);
#25005=ORIENTED_EDGE('',*,*,#17329,.T.);
#25006=ORIENTED_EDGE('',*,*,#17221,.T.);
#25007=ORIENTED_EDGE('',*,*,#16744,.T.);
#25008=ORIENTED_EDGE('',*,*,#16740,.T.);
#25009=ORIENTED_EDGE('',*,*,#16737,.T.);
#25010=ORIENTED_EDGE('',*,*,#16734,.T.);
#25011=ORIENTED_EDGE('',*,*,#17330,.T.);
#25012=ORIENTED_EDGE('',*,*,#16137,.T.);
#25013=ORIENTED_EDGE('',*,*,#16142,.T.);
#25014=ORIENTED_EDGE('',*,*,#16141,.T.);
#25015=ORIENTED_EDGE('',*,*,#16147,.T.);
#25016=ORIENTED_EDGE('',*,*,#16146,.T.);
#25017=ORIENTED_EDGE('',*,*,#16152,.T.);
#25018=ORIENTED_EDGE('',*,*,#16151,.T.);
#25019=ORIENTED_EDGE('',*,*,#17255,.T.);
#25020=ORIENTED_EDGE('',*,*,#17254,.T.);
#25021=ORIENTED_EDGE('',*,*,#17331,.T.);
#25022=ORIENTED_EDGE('',*,*,#17252,.F.);
#25023=ORIENTED_EDGE('',*,*,#17251,.F.);
#25024=ORIENTED_EDGE('',*,*,#16154,.F.);
#25025=ORIENTED_EDGE('',*,*,#16153,.F.);
#25026=ORIENTED_EDGE('',*,*,#16149,.F.);
#25027=ORIENTED_EDGE('',*,*,#16148,.F.);
#25028=ORIENTED_EDGE('',*,*,#16144,.F.);
#25029=ORIENTED_EDGE('',*,*,#16143,.F.);
#25030=ORIENTED_EDGE('',*,*,#16139,.F.);
#25031=ORIENTED_EDGE('',*,*,#17332,.T.);
#25032=ORIENTED_EDGE('',*,*,#16732,.T.);
#25033=ORIENTED_EDGE('',*,*,#16736,.T.);
#25034=ORIENTED_EDGE('',*,*,#16739,.T.);
#25035=ORIENTED_EDGE('',*,*,#16743,.T.);
#25036=ORIENTED_EDGE('',*,*,#17333,.T.);
#25037=ORIENTED_EDGE('',*,*,#16719,.T.);
#25038=ORIENTED_EDGE('',*,*,#16722,.T.);
#25039=ORIENTED_EDGE('',*,*,#16726,.T.);
#25040=ORIENTED_EDGE('',*,*,#16729,.T.);
#25041=ORIENTED_EDGE('',*,*,#17225,.T.);
#25042=ORIENTED_EDGE('',*,*,#17334,.T.);
#25043=ORIENTED_EDGE('',*,*,#16156,.T.);
#25044=ORIENTED_EDGE('',*,*,#16161,.T.);
#25045=ORIENTED_EDGE('',*,*,#16160,.T.);
#25046=ORIENTED_EDGE('',*,*,#16166,.T.);
#25047=ORIENTED_EDGE('',*,*,#16165,.T.);
#25048=ORIENTED_EDGE('',*,*,#16171,.T.);
#25049=ORIENTED_EDGE('',*,*,#16170,.T.);
#25050=ORIENTED_EDGE('',*,*,#17250,.T.);
#25051=ORIENTED_EDGE('',*,*,#17249,.T.);
#25052=ORIENTED_EDGE('',*,*,#17335,.T.);
#25053=ORIENTED_EDGE('',*,*,#17247,.F.);
#25054=ORIENTED_EDGE('',*,*,#17246,.F.);
#25055=ORIENTED_EDGE('',*,*,#16173,.F.);
#25056=ORIENTED_EDGE('',*,*,#16172,.F.);
#25057=ORIENTED_EDGE('',*,*,#16168,.F.);
#25058=ORIENTED_EDGE('',*,*,#16167,.F.);
#25059=ORIENTED_EDGE('',*,*,#16163,.F.);
#25060=ORIENTED_EDGE('',*,*,#16162,.F.);
#25061=ORIENTED_EDGE('',*,*,#16158,.F.);
#25062=ORIENTED_EDGE('',*,*,#17336,.T.);
#25063=ORIENTED_EDGE('',*,*,#17223,.T.);
#25064=ORIENTED_EDGE('',*,*,#16730,.T.);
#25065=ORIENTED_EDGE('',*,*,#16727,.T.);
#25066=ORIENTED_EDGE('',*,*,#16724,.T.);
#25067=ORIENTED_EDGE('',*,*,#17322,.T.);
#25068=ORIENTED_EDGE('',*,*,#17209,.T.);
#25069=ORIENTED_EDGE('',*,*,#17208,.T.);
#25070=ORIENTED_EDGE('',*,*,#17207,.T.);
#25071=ORIENTED_EDGE('',*,*,#17203,.T.);
#25072=ORIENTED_EDGE('',*,*,#17202,.T.);
#25073=ORIENTED_EDGE('',*,*,#17199,.T.);
#25074=ORIENTED_EDGE('',*,*,#17195,.T.);
#25075=ORIENTED_EDGE('',*,*,#17194,.T.);
#25076=ORIENTED_EDGE('',*,*,#17190,.T.);
#25077=ORIENTED_EDGE('',*,*,#17187,.T.);
#25078=ORIENTED_EDGE('',*,*,#17186,.T.);
#25079=ORIENTED_EDGE('',*,*,#17182,.T.);
#25080=ORIENTED_EDGE('',*,*,#17179,.T.);
#25081=ORIENTED_EDGE('',*,*,#17178,.T.);
#25082=ORIENTED_EDGE('',*,*,#17174,.T.);
#25083=ORIENTED_EDGE('',*,*,#17170,.T.);
#25084=ORIENTED_EDGE('',*,*,#17169,.T.);
#25085=ORIENTED_EDGE('',*,*,#17165,.T.);
#25086=ORIENTED_EDGE('',*,*,#17162,.T.);
#25087=ORIENTED_EDGE('',*,*,#17161,.T.);
#25088=ORIENTED_EDGE('',*,*,#17157,.T.);
#25089=ORIENTED_EDGE('',*,*,#17156,.T.);
#25090=ORIENTED_EDGE('',*,*,#17153,.T.);
#25091=ORIENTED_EDGE('',*,*,#17152,.T.);
#25092=ORIENTED_EDGE('',*,*,#17148,.T.);
#25093=ORIENTED_EDGE('',*,*,#17144,.T.);
#25094=ORIENTED_EDGE('',*,*,#17143,.T.);
#25095=ORIENTED_EDGE('',*,*,#17139,.T.);
#25096=ORIENTED_EDGE('',*,*,#17136,.T.);
#25097=ORIENTED_EDGE('',*,*,#17135,.T.);
#25098=ORIENTED_EDGE('',*,*,#17131,.T.);
#25099=ORIENTED_EDGE('',*,*,#17130,.T.);
#25100=ORIENTED_EDGE('',*,*,#17127,.T.);
#25101=ORIENTED_EDGE('',*,*,#17126,.T.);
#25102=ORIENTED_EDGE('',*,*,#17122,.T.);
#25103=ORIENTED_EDGE('',*,*,#17119,.T.);
#25104=ORIENTED_EDGE('',*,*,#17118,.T.);
#25105=ORIENTED_EDGE('',*,*,#17114,.T.);
#25106=ORIENTED_EDGE('',*,*,#17111,.T.);
#25107=ORIENTED_EDGE('',*,*,#17110,.T.);
#25108=ORIENTED_EDGE('',*,*,#17106,.T.);
#25109=ORIENTED_EDGE('',*,*,#17105,.T.);
#25110=ORIENTED_EDGE('',*,*,#17102,.T.);
#25111=ORIENTED_EDGE('',*,*,#17098,.T.);
#25112=ORIENTED_EDGE('',*,*,#17097,.T.);
#25113=ORIENTED_EDGE('',*,*,#17337,.T.);
#25114=ORIENTED_EDGE('',*,*,#16176,.T.);
#25115=ORIENTED_EDGE('',*,*,#16175,.T.);
#25116=ORIENTED_EDGE('',*,*,#16182,.T.);
#25117=ORIENTED_EDGE('',*,*,#16181,.T.);
#25118=ORIENTED_EDGE('',*,*,#16187,.T.);
#25119=ORIENTED_EDGE('',*,*,#16186,.T.);
#25120=ORIENTED_EDGE('',*,*,#16192,.T.);
#25121=ORIENTED_EDGE('',*,*,#16191,.T.);
#25122=ORIENTED_EDGE('',*,*,#16197,.T.);
#25123=ORIENTED_EDGE('',*,*,#16196,.T.);
#25124=ORIENTED_EDGE('',*,*,#16202,.T.);
#25125=ORIENTED_EDGE('',*,*,#16201,.T.);
#25126=ORIENTED_EDGE('',*,*,#16207,.T.);
#25127=ORIENTED_EDGE('',*,*,#16206,.T.);
#25128=ORIENTED_EDGE('',*,*,#16212,.T.);
#25129=ORIENTED_EDGE('',*,*,#16211,.T.);
#25130=ORIENTED_EDGE('',*,*,#16217,.T.);
#25131=ORIENTED_EDGE('',*,*,#16216,.T.);
#25132=ORIENTED_EDGE('',*,*,#16222,.T.);
#25133=ORIENTED_EDGE('',*,*,#16221,.T.);
#25134=ORIENTED_EDGE('',*,*,#16227,.T.);
#25135=ORIENTED_EDGE('',*,*,#16226,.T.);
#25136=ORIENTED_EDGE('',*,*,#16232,.T.);
#25137=ORIENTED_EDGE('',*,*,#16231,.T.);
#25138=ORIENTED_EDGE('',*,*,#16237,.T.);
#25139=ORIENTED_EDGE('',*,*,#16236,.T.);
#25140=ORIENTED_EDGE('',*,*,#16242,.T.);
#25141=ORIENTED_EDGE('',*,*,#16241,.T.);
#25142=ORIENTED_EDGE('',*,*,#16247,.T.);
#25143=ORIENTED_EDGE('',*,*,#16246,.T.);
#25144=ORIENTED_EDGE('',*,*,#16252,.T.);
#25145=ORIENTED_EDGE('',*,*,#16251,.T.);
#25146=ORIENTED_EDGE('',*,*,#16257,.T.);
#25147=ORIENTED_EDGE('',*,*,#16256,.T.);
#25148=ORIENTED_EDGE('',*,*,#16262,.T.);
#25149=ORIENTED_EDGE('',*,*,#16261,.T.);
#25150=ORIENTED_EDGE('',*,*,#16267,.T.);
#25151=ORIENTED_EDGE('',*,*,#16266,.T.);
#25152=ORIENTED_EDGE('',*,*,#16272,.T.);
#25153=ORIENTED_EDGE('',*,*,#16271,.T.);
#25154=ORIENTED_EDGE('',*,*,#16277,.T.);
#25155=ORIENTED_EDGE('',*,*,#16276,.T.);
#25156=ORIENTED_EDGE('',*,*,#16282,.T.);
#25157=ORIENTED_EDGE('',*,*,#16281,.T.);
#25158=ORIENTED_EDGE('',*,*,#16287,.T.);
#25159=ORIENTED_EDGE('',*,*,#16286,.T.);
#25160=ORIENTED_EDGE('',*,*,#16292,.T.);
#25161=ORIENTED_EDGE('',*,*,#16291,.T.);
#25162=ORIENTED_EDGE('',*,*,#16297,.T.);
#25163=ORIENTED_EDGE('',*,*,#16296,.T.);
#25164=ORIENTED_EDGE('',*,*,#16302,.T.);
#25165=ORIENTED_EDGE('',*,*,#16301,.T.);
#25166=ORIENTED_EDGE('',*,*,#16307,.T.);
#25167=ORIENTED_EDGE('',*,*,#16306,.T.);
#25168=ORIENTED_EDGE('',*,*,#17245,.T.);
#25169=ORIENTED_EDGE('',*,*,#17244,.T.);
#25170=ORIENTED_EDGE('',*,*,#17321,.T.);
#25171=ORIENTED_EDGE('',*,*,#17242,.F.);
#25172=ORIENTED_EDGE('',*,*,#17241,.F.);
#25173=ORIENTED_EDGE('',*,*,#16309,.F.);
#25174=ORIENTED_EDGE('',*,*,#16308,.F.);
#25175=ORIENTED_EDGE('',*,*,#16304,.F.);
#25176=ORIENTED_EDGE('',*,*,#16303,.F.);
#25177=ORIENTED_EDGE('',*,*,#16299,.F.);
#25178=ORIENTED_EDGE('',*,*,#16298,.F.);
#25179=ORIENTED_EDGE('',*,*,#16294,.F.);
#25180=ORIENTED_EDGE('',*,*,#16293,.F.);
#25181=ORIENTED_EDGE('',*,*,#16289,.F.);
#25182=ORIENTED_EDGE('',*,*,#16288,.F.);
#25183=ORIENTED_EDGE('',*,*,#16284,.F.);
#25184=ORIENTED_EDGE('',*,*,#16283,.F.);
#25185=ORIENTED_EDGE('',*,*,#16279,.F.);
#25186=ORIENTED_EDGE('',*,*,#16278,.F.);
#25187=ORIENTED_EDGE('',*,*,#16274,.F.);
#25188=ORIENTED_EDGE('',*,*,#16273,.F.);
#25189=ORIENTED_EDGE('',*,*,#16269,.F.);
#25190=ORIENTED_EDGE('',*,*,#16268,.F.);
#25191=ORIENTED_EDGE('',*,*,#16264,.F.);
#25192=ORIENTED_EDGE('',*,*,#16263,.F.);
#25193=ORIENTED_EDGE('',*,*,#16259,.F.);
#25194=ORIENTED_EDGE('',*,*,#16258,.F.);
#25195=ORIENTED_EDGE('',*,*,#16254,.F.);
#25196=ORIENTED_EDGE('',*,*,#16253,.F.);
#25197=ORIENTED_EDGE('',*,*,#16249,.F.);
#25198=ORIENTED_EDGE('',*,*,#16248,.F.);
#25199=ORIENTED_EDGE('',*,*,#16244,.F.);
#25200=ORIENTED_EDGE('',*,*,#16243,.F.);
#25201=ORIENTED_EDGE('',*,*,#16239,.F.);
#25202=ORIENTED_EDGE('',*,*,#16238,.F.);
#25203=ORIENTED_EDGE('',*,*,#16234,.F.);
#25204=ORIENTED_EDGE('',*,*,#16233,.F.);
#25205=ORIENTED_EDGE('',*,*,#16229,.F.);
#25206=ORIENTED_EDGE('',*,*,#16228,.F.);
#25207=ORIENTED_EDGE('',*,*,#16224,.F.);
#25208=ORIENTED_EDGE('',*,*,#16223,.F.);
#25209=ORIENTED_EDGE('',*,*,#16219,.F.);
#25210=ORIENTED_EDGE('',*,*,#16218,.F.);
#25211=ORIENTED_EDGE('',*,*,#16214,.F.);
#25212=ORIENTED_EDGE('',*,*,#16213,.F.);
#25213=ORIENTED_EDGE('',*,*,#16209,.F.);
#25214=ORIENTED_EDGE('',*,*,#16208,.F.);
#25215=ORIENTED_EDGE('',*,*,#16204,.F.);
#25216=ORIENTED_EDGE('',*,*,#16203,.F.);
#25217=ORIENTED_EDGE('',*,*,#16199,.F.);
#25218=ORIENTED_EDGE('',*,*,#16198,.F.);
#25219=ORIENTED_EDGE('',*,*,#16194,.F.);
#25220=ORIENTED_EDGE('',*,*,#16193,.F.);
#25221=ORIENTED_EDGE('',*,*,#16189,.F.);
#25222=ORIENTED_EDGE('',*,*,#16188,.F.);
#25223=ORIENTED_EDGE('',*,*,#16184,.F.);
#25224=ORIENTED_EDGE('',*,*,#16183,.F.);
#25225=ORIENTED_EDGE('',*,*,#16179,.F.);
#25226=ORIENTED_EDGE('',*,*,#16178,.F.);
#25227=ORIENTED_EDGE('',*,*,#17338,.T.);
#25228=ORIENTED_EDGE('',*,*,#17095,.T.);
#25229=ORIENTED_EDGE('',*,*,#17094,.T.);
#25230=ORIENTED_EDGE('',*,*,#17101,.T.);
#25231=ORIENTED_EDGE('',*,*,#17100,.T.);
#25232=ORIENTED_EDGE('',*,*,#17104,.T.);
#25233=ORIENTED_EDGE('',*,*,#17109,.T.);
#25234=ORIENTED_EDGE('',*,*,#17108,.T.);
#25235=ORIENTED_EDGE('',*,*,#17113,.T.);
#25236=ORIENTED_EDGE('',*,*,#17117,.T.);
#25237=ORIENTED_EDGE('',*,*,#17116,.T.);
#25238=ORIENTED_EDGE('',*,*,#17121,.T.);
#25239=ORIENTED_EDGE('',*,*,#17125,.T.);
#25240=ORIENTED_EDGE('',*,*,#17124,.T.);
#25241=ORIENTED_EDGE('',*,*,#17129,.T.);
#25242=ORIENTED_EDGE('',*,*,#17134,.T.);
#25243=ORIENTED_EDGE('',*,*,#17133,.T.);
#25244=ORIENTED_EDGE('',*,*,#17138,.T.);
#25245=ORIENTED_EDGE('',*,*,#17142,.T.);
#25246=ORIENTED_EDGE('',*,*,#17141,.T.);
#25247=ORIENTED_EDGE('',*,*,#17147,.T.);
#25248=ORIENTED_EDGE('',*,*,#17146,.T.);
#25249=ORIENTED_EDGE('',*,*,#17151,.T.);
#25250=ORIENTED_EDGE('',*,*,#17150,.T.);
#25251=ORIENTED_EDGE('',*,*,#17155,.T.);
#25252=ORIENTED_EDGE('',*,*,#17160,.T.);
#25253=ORIENTED_EDGE('',*,*,#17159,.T.);
#25254=ORIENTED_EDGE('',*,*,#17164,.T.);
#25255=ORIENTED_EDGE('',*,*,#17168,.T.);
#25256=ORIENTED_EDGE('',*,*,#17167,.T.);
#25257=ORIENTED_EDGE('',*,*,#17173,.T.);
#25258=ORIENTED_EDGE('',*,*,#17172,.T.);
#25259=ORIENTED_EDGE('',*,*,#17177,.T.);
#25260=ORIENTED_EDGE('',*,*,#17176,.T.);
#25261=ORIENTED_EDGE('',*,*,#17181,.T.);
#25262=ORIENTED_EDGE('',*,*,#17185,.T.);
#25263=ORIENTED_EDGE('',*,*,#17184,.T.);
#25264=ORIENTED_EDGE('',*,*,#17189,.T.);
#25265=ORIENTED_EDGE('',*,*,#17193,.T.);
#25266=ORIENTED_EDGE('',*,*,#17192,.T.);
#25267=ORIENTED_EDGE('',*,*,#17198,.T.);
#25268=ORIENTED_EDGE('',*,*,#17197,.T.);
#25269=ORIENTED_EDGE('',*,*,#17201,.T.);
#25270=ORIENTED_EDGE('',*,*,#17206,.T.);
#25271=ORIENTED_EDGE('',*,*,#17205,.T.);
#25272=ORIENTED_EDGE('',*,*,#17211,.T.);
#25273=ORIENTED_EDGE('',*,*,#17324,.T.);
#25274=ORIENTED_EDGE('',*,*,#17212,.T.);
#25275=ORIENTED_EDGE('',*,*,#17092,.T.);
#25276=ORIENTED_EDGE('',*,*,#17091,.T.);
#25277=ORIENTED_EDGE('',*,*,#17087,.T.);
#25278=ORIENTED_EDGE('',*,*,#17086,.T.);
#25279=ORIENTED_EDGE('',*,*,#17083,.T.);
#25280=ORIENTED_EDGE('',*,*,#17079,.T.);
#25281=ORIENTED_EDGE('',*,*,#17078,.T.);
#25282=ORIENTED_EDGE('',*,*,#17074,.T.);
#25283=ORIENTED_EDGE('',*,*,#17071,.T.);
#25284=ORIENTED_EDGE('',*,*,#17070,.T.);
#25285=ORIENTED_EDGE('',*,*,#17066,.T.);
#25286=ORIENTED_EDGE('',*,*,#17063,.T.);
#25287=ORIENTED_EDGE('',*,*,#17062,.T.);
#25288=ORIENTED_EDGE('',*,*,#17058,.T.);
#25289=ORIENTED_EDGE('',*,*,#17054,.T.);
#25290=ORIENTED_EDGE('',*,*,#17053,.T.);
#25291=ORIENTED_EDGE('',*,*,#17049,.T.);
#25292=ORIENTED_EDGE('',*,*,#17046,.T.);
#25293=ORIENTED_EDGE('',*,*,#17045,.T.);
#25294=ORIENTED_EDGE('',*,*,#17041,.T.);
#25295=ORIENTED_EDGE('',*,*,#17040,.T.);
#25296=ORIENTED_EDGE('',*,*,#17037,.T.);
#25297=ORIENTED_EDGE('',*,*,#17036,.T.);
#25298=ORIENTED_EDGE('',*,*,#17032,.T.);
#25299=ORIENTED_EDGE('',*,*,#17028,.T.);
#25300=ORIENTED_EDGE('',*,*,#17027,.T.);
#25301=ORIENTED_EDGE('',*,*,#17023,.T.);
#25302=ORIENTED_EDGE('',*,*,#17020,.T.);
#25303=ORIENTED_EDGE('',*,*,#17019,.T.);
#25304=ORIENTED_EDGE('',*,*,#17015,.T.);
#25305=ORIENTED_EDGE('',*,*,#17014,.T.);
#25306=ORIENTED_EDGE('',*,*,#17011,.T.);
#25307=ORIENTED_EDGE('',*,*,#17010,.T.);
#25308=ORIENTED_EDGE('',*,*,#17006,.T.);
#25309=ORIENTED_EDGE('',*,*,#17003,.T.);
#25310=ORIENTED_EDGE('',*,*,#17002,.T.);
#25311=ORIENTED_EDGE('',*,*,#16998,.T.);
#25312=ORIENTED_EDGE('',*,*,#16995,.T.);
#25313=ORIENTED_EDGE('',*,*,#16994,.T.);
#25314=ORIENTED_EDGE('',*,*,#16990,.T.);
#25315=ORIENTED_EDGE('',*,*,#16989,.T.);
#25316=ORIENTED_EDGE('',*,*,#16986,.T.);
#25317=ORIENTED_EDGE('',*,*,#16982,.T.);
#25318=ORIENTED_EDGE('',*,*,#16981,.T.);
#25319=ORIENTED_EDGE('',*,*,#17339,.T.);
#25320=ORIENTED_EDGE('',*,*,#16312,.T.);
#25321=ORIENTED_EDGE('',*,*,#16311,.T.);
#25322=ORIENTED_EDGE('',*,*,#16318,.T.);
#25323=ORIENTED_EDGE('',*,*,#16317,.T.);
#25324=ORIENTED_EDGE('',*,*,#16323,.T.);
#25325=ORIENTED_EDGE('',*,*,#16322,.T.);
#25326=ORIENTED_EDGE('',*,*,#16328,.T.);
#25327=ORIENTED_EDGE('',*,*,#16327,.T.);
#25328=ORIENTED_EDGE('',*,*,#16333,.T.);
#25329=ORIENTED_EDGE('',*,*,#16332,.T.);
#25330=ORIENTED_EDGE('',*,*,#16338,.T.);
#25331=ORIENTED_EDGE('',*,*,#16337,.T.);
#25332=ORIENTED_EDGE('',*,*,#16343,.T.);
#25333=ORIENTED_EDGE('',*,*,#16342,.T.);
#25334=ORIENTED_EDGE('',*,*,#16348,.T.);
#25335=ORIENTED_EDGE('',*,*,#16347,.T.);
#25336=ORIENTED_EDGE('',*,*,#16353,.T.);
#25337=ORIENTED_EDGE('',*,*,#16352,.T.);
#25338=ORIENTED_EDGE('',*,*,#16358,.T.);
#25339=ORIENTED_EDGE('',*,*,#16357,.T.);
#25340=ORIENTED_EDGE('',*,*,#16363,.T.);
#25341=ORIENTED_EDGE('',*,*,#16362,.T.);
#25342=ORIENTED_EDGE('',*,*,#16368,.T.);
#25343=ORIENTED_EDGE('',*,*,#16367,.T.);
#25344=ORIENTED_EDGE('',*,*,#16373,.T.);
#25345=ORIENTED_EDGE('',*,*,#16372,.T.);
#25346=ORIENTED_EDGE('',*,*,#16378,.T.);
#25347=ORIENTED_EDGE('',*,*,#16377,.T.);
#25348=ORIENTED_EDGE('',*,*,#16383,.T.);
#25349=ORIENTED_EDGE('',*,*,#16382,.T.);
#25350=ORIENTED_EDGE('',*,*,#16388,.T.);
#25351=ORIENTED_EDGE('',*,*,#16387,.T.);
#25352=ORIENTED_EDGE('',*,*,#16393,.T.);
#25353=ORIENTED_EDGE('',*,*,#16392,.T.);
#25354=ORIENTED_EDGE('',*,*,#16398,.T.);
#25355=ORIENTED_EDGE('',*,*,#16397,.T.);
#25356=ORIENTED_EDGE('',*,*,#16403,.T.);
#25357=ORIENTED_EDGE('',*,*,#16402,.T.);
#25358=ORIENTED_EDGE('',*,*,#16408,.T.);
#25359=ORIENTED_EDGE('',*,*,#16407,.T.);
#25360=ORIENTED_EDGE('',*,*,#16413,.T.);
#25361=ORIENTED_EDGE('',*,*,#16412,.T.);
#25362=ORIENTED_EDGE('',*,*,#16418,.T.);
#25363=ORIENTED_EDGE('',*,*,#16417,.T.);
#25364=ORIENTED_EDGE('',*,*,#16423,.T.);
#25365=ORIENTED_EDGE('',*,*,#16422,.T.);
#25366=ORIENTED_EDGE('',*,*,#16428,.T.);
#25367=ORIENTED_EDGE('',*,*,#16427,.T.);
#25368=ORIENTED_EDGE('',*,*,#16433,.T.);
#25369=ORIENTED_EDGE('',*,*,#16432,.T.);
#25370=ORIENTED_EDGE('',*,*,#16438,.T.);
#25371=ORIENTED_EDGE('',*,*,#16437,.T.);
#25372=ORIENTED_EDGE('',*,*,#16443,.T.);
#25373=ORIENTED_EDGE('',*,*,#16442,.T.);
#25374=ORIENTED_EDGE('',*,*,#17240,.T.);
#25375=ORIENTED_EDGE('',*,*,#17239,.T.);
#25376=ORIENTED_EDGE('',*,*,#17323,.T.);
#25377=ORIENTED_EDGE('',*,*,#17237,.F.);
#25378=ORIENTED_EDGE('',*,*,#17236,.F.);
#25379=ORIENTED_EDGE('',*,*,#16445,.F.);
#25380=ORIENTED_EDGE('',*,*,#16444,.F.);
#25381=ORIENTED_EDGE('',*,*,#16440,.F.);
#25382=ORIENTED_EDGE('',*,*,#16439,.F.);
#25383=ORIENTED_EDGE('',*,*,#16435,.F.);
#25384=ORIENTED_EDGE('',*,*,#16434,.F.);
#25385=ORIENTED_EDGE('',*,*,#16430,.F.);
#25386=ORIENTED_EDGE('',*,*,#16429,.F.);
#25387=ORIENTED_EDGE('',*,*,#16425,.F.);
#25388=ORIENTED_EDGE('',*,*,#16424,.F.);
#25389=ORIENTED_EDGE('',*,*,#16420,.F.);
#25390=ORIENTED_EDGE('',*,*,#16419,.F.);
#25391=ORIENTED_EDGE('',*,*,#16415,.F.);
#25392=ORIENTED_EDGE('',*,*,#16414,.F.);
#25393=ORIENTED_EDGE('',*,*,#16410,.F.);
#25394=ORIENTED_EDGE('',*,*,#16409,.F.);
#25395=ORIENTED_EDGE('',*,*,#16405,.F.);
#25396=ORIENTED_EDGE('',*,*,#16404,.F.);
#25397=ORIENTED_EDGE('',*,*,#16400,.F.);
#25398=ORIENTED_EDGE('',*,*,#16399,.F.);
#25399=ORIENTED_EDGE('',*,*,#16395,.F.);
#25400=ORIENTED_EDGE('',*,*,#16394,.F.);
#25401=ORIENTED_EDGE('',*,*,#16390,.F.);
#25402=ORIENTED_EDGE('',*,*,#16389,.F.);
#25403=ORIENTED_EDGE('',*,*,#16385,.F.);
#25404=ORIENTED_EDGE('',*,*,#16384,.F.);
#25405=ORIENTED_EDGE('',*,*,#16380,.F.);
#25406=ORIENTED_EDGE('',*,*,#16379,.F.);
#25407=ORIENTED_EDGE('',*,*,#16375,.F.);
#25408=ORIENTED_EDGE('',*,*,#16374,.F.);
#25409=ORIENTED_EDGE('',*,*,#16370,.F.);
#25410=ORIENTED_EDGE('',*,*,#16369,.F.);
#25411=ORIENTED_EDGE('',*,*,#16365,.F.);
#25412=ORIENTED_EDGE('',*,*,#16364,.F.);
#25413=ORIENTED_EDGE('',*,*,#16360,.F.);
#25414=ORIENTED_EDGE('',*,*,#16359,.F.);
#25415=ORIENTED_EDGE('',*,*,#16355,.F.);
#25416=ORIENTED_EDGE('',*,*,#16354,.F.);
#25417=ORIENTED_EDGE('',*,*,#16350,.F.);
#25418=ORIENTED_EDGE('',*,*,#16349,.F.);
#25419=ORIENTED_EDGE('',*,*,#16345,.F.);
#25420=ORIENTED_EDGE('',*,*,#16344,.F.);
#25421=ORIENTED_EDGE('',*,*,#16340,.F.);
#25422=ORIENTED_EDGE('',*,*,#16339,.F.);
#25423=ORIENTED_EDGE('',*,*,#16335,.F.);
#25424=ORIENTED_EDGE('',*,*,#16334,.F.);
#25425=ORIENTED_EDGE('',*,*,#16330,.F.);
#25426=ORIENTED_EDGE('',*,*,#16329,.F.);
#25427=ORIENTED_EDGE('',*,*,#16325,.F.);
#25428=ORIENTED_EDGE('',*,*,#16324,.F.);
#25429=ORIENTED_EDGE('',*,*,#16320,.F.);
#25430=ORIENTED_EDGE('',*,*,#16319,.F.);
#25431=ORIENTED_EDGE('',*,*,#16315,.F.);
#25432=ORIENTED_EDGE('',*,*,#16314,.F.);
#25433=ORIENTED_EDGE('',*,*,#17340,.T.);
#25434=ORIENTED_EDGE('',*,*,#16979,.T.);
#25435=ORIENTED_EDGE('',*,*,#16978,.T.);
#25436=ORIENTED_EDGE('',*,*,#16985,.T.);
#25437=ORIENTED_EDGE('',*,*,#16984,.T.);
#25438=ORIENTED_EDGE('',*,*,#16988,.T.);
#25439=ORIENTED_EDGE('',*,*,#16993,.T.);
#25440=ORIENTED_EDGE('',*,*,#16992,.T.);
#25441=ORIENTED_EDGE('',*,*,#16997,.T.);
#25442=ORIENTED_EDGE('',*,*,#17001,.T.);
#25443=ORIENTED_EDGE('',*,*,#17000,.T.);
#25444=ORIENTED_EDGE('',*,*,#17005,.T.);
#25445=ORIENTED_EDGE('',*,*,#17009,.T.);
#25446=ORIENTED_EDGE('',*,*,#17008,.T.);
#25447=ORIENTED_EDGE('',*,*,#17013,.T.);
#25448=ORIENTED_EDGE('',*,*,#17018,.T.);
#25449=ORIENTED_EDGE('',*,*,#17017,.T.);
#25450=ORIENTED_EDGE('',*,*,#17022,.T.);
#25451=ORIENTED_EDGE('',*,*,#17026,.T.);
#25452=ORIENTED_EDGE('',*,*,#17025,.T.);
#25453=ORIENTED_EDGE('',*,*,#17031,.T.);
#25454=ORIENTED_EDGE('',*,*,#17030,.T.);
#25455=ORIENTED_EDGE('',*,*,#17035,.T.);
#25456=ORIENTED_EDGE('',*,*,#17034,.T.);
#25457=ORIENTED_EDGE('',*,*,#17039,.T.);
#25458=ORIENTED_EDGE('',*,*,#17044,.T.);
#25459=ORIENTED_EDGE('',*,*,#17043,.T.);
#25460=ORIENTED_EDGE('',*,*,#17048,.T.);
#25461=ORIENTED_EDGE('',*,*,#17052,.T.);
#25462=ORIENTED_EDGE('',*,*,#17051,.T.);
#25463=ORIENTED_EDGE('',*,*,#17057,.T.);
#25464=ORIENTED_EDGE('',*,*,#17056,.T.);
#25465=ORIENTED_EDGE('',*,*,#17061,.T.);
#25466=ORIENTED_EDGE('',*,*,#17060,.T.);
#25467=ORIENTED_EDGE('',*,*,#17065,.T.);
#25468=ORIENTED_EDGE('',*,*,#17069,.T.);
#25469=ORIENTED_EDGE('',*,*,#17068,.T.);
#25470=ORIENTED_EDGE('',*,*,#17073,.T.);
#25471=ORIENTED_EDGE('',*,*,#17077,.T.);
#25472=ORIENTED_EDGE('',*,*,#17076,.T.);
#25473=ORIENTED_EDGE('',*,*,#17082,.T.);
#25474=ORIENTED_EDGE('',*,*,#17081,.T.);
#25475=ORIENTED_EDGE('',*,*,#17085,.T.);
#25476=ORIENTED_EDGE('',*,*,#17090,.T.);
#25477=ORIENTED_EDGE('',*,*,#17089,.T.);
#25478=ORIENTED_EDGE('',*,*,#17214,.T.);
#25479=ORIENTED_EDGE('',*,*,#17326,.T.);
#25480=ORIENTED_EDGE('',*,*,#17215,.T.);
#25481=ORIENTED_EDGE('',*,*,#16976,.T.);
#25482=ORIENTED_EDGE('',*,*,#16975,.T.);
#25483=ORIENTED_EDGE('',*,*,#16971,.T.);
#25484=ORIENTED_EDGE('',*,*,#16970,.T.);
#25485=ORIENTED_EDGE('',*,*,#16967,.T.);
#25486=ORIENTED_EDGE('',*,*,#16963,.T.);
#25487=ORIENTED_EDGE('',*,*,#16962,.T.);
#25488=ORIENTED_EDGE('',*,*,#16958,.T.);
#25489=ORIENTED_EDGE('',*,*,#16955,.T.);
#25490=ORIENTED_EDGE('',*,*,#16954,.T.);
#25491=ORIENTED_EDGE('',*,*,#16950,.T.);
#25492=ORIENTED_EDGE('',*,*,#16947,.T.);
#25493=ORIENTED_EDGE('',*,*,#16946,.T.);
#25494=ORIENTED_EDGE('',*,*,#16942,.T.);
#25495=ORIENTED_EDGE('',*,*,#16938,.T.);
#25496=ORIENTED_EDGE('',*,*,#16937,.T.);
#25497=ORIENTED_EDGE('',*,*,#16933,.T.);
#25498=ORIENTED_EDGE('',*,*,#16930,.T.);
#25499=ORIENTED_EDGE('',*,*,#16929,.T.);
#25500=ORIENTED_EDGE('',*,*,#16925,.T.);
#25501=ORIENTED_EDGE('',*,*,#16924,.T.);
#25502=ORIENTED_EDGE('',*,*,#16921,.T.);
#25503=ORIENTED_EDGE('',*,*,#16920,.T.);
#25504=ORIENTED_EDGE('',*,*,#16916,.T.);
#25505=ORIENTED_EDGE('',*,*,#16912,.T.);
#25506=ORIENTED_EDGE('',*,*,#16911,.T.);
#25507=ORIENTED_EDGE('',*,*,#16907,.T.);
#25508=ORIENTED_EDGE('',*,*,#16904,.T.);
#25509=ORIENTED_EDGE('',*,*,#16903,.T.);
#25510=ORIENTED_EDGE('',*,*,#16899,.T.);
#25511=ORIENTED_EDGE('',*,*,#16898,.T.);
#25512=ORIENTED_EDGE('',*,*,#16895,.T.);
#25513=ORIENTED_EDGE('',*,*,#16894,.T.);
#25514=ORIENTED_EDGE('',*,*,#16890,.T.);
#25515=ORIENTED_EDGE('',*,*,#16887,.T.);
#25516=ORIENTED_EDGE('',*,*,#16886,.T.);
#25517=ORIENTED_EDGE('',*,*,#16882,.T.);
#25518=ORIENTED_EDGE('',*,*,#16879,.T.);
#25519=ORIENTED_EDGE('',*,*,#16878,.T.);
#25520=ORIENTED_EDGE('',*,*,#16874,.T.);
#25521=ORIENTED_EDGE('',*,*,#16873,.T.);
#25522=ORIENTED_EDGE('',*,*,#16870,.T.);
#25523=ORIENTED_EDGE('',*,*,#16866,.T.);
#25524=ORIENTED_EDGE('',*,*,#16865,.T.);
#25525=ORIENTED_EDGE('',*,*,#17341,.T.);
#25526=ORIENTED_EDGE('',*,*,#16448,.T.);
#25527=ORIENTED_EDGE('',*,*,#16447,.T.);
#25528=ORIENTED_EDGE('',*,*,#16454,.T.);
#25529=ORIENTED_EDGE('',*,*,#16453,.T.);
#25530=ORIENTED_EDGE('',*,*,#16459,.T.);
#25531=ORIENTED_EDGE('',*,*,#16458,.T.);
#25532=ORIENTED_EDGE('',*,*,#16464,.T.);
#25533=ORIENTED_EDGE('',*,*,#16463,.T.);
#25534=ORIENTED_EDGE('',*,*,#16469,.T.);
#25535=ORIENTED_EDGE('',*,*,#16468,.T.);
#25536=ORIENTED_EDGE('',*,*,#16474,.T.);
#25537=ORIENTED_EDGE('',*,*,#16473,.T.);
#25538=ORIENTED_EDGE('',*,*,#16479,.T.);
#25539=ORIENTED_EDGE('',*,*,#16478,.T.);
#25540=ORIENTED_EDGE('',*,*,#16484,.T.);
#25541=ORIENTED_EDGE('',*,*,#16483,.T.);
#25542=ORIENTED_EDGE('',*,*,#16489,.T.);
#25543=ORIENTED_EDGE('',*,*,#16488,.T.);
#25544=ORIENTED_EDGE('',*,*,#16494,.T.);
#25545=ORIENTED_EDGE('',*,*,#16493,.T.);
#25546=ORIENTED_EDGE('',*,*,#16499,.T.);
#25547=ORIENTED_EDGE('',*,*,#16498,.T.);
#25548=ORIENTED_EDGE('',*,*,#16504,.T.);
#25549=ORIENTED_EDGE('',*,*,#16503,.T.);
#25550=ORIENTED_EDGE('',*,*,#16509,.T.);
#25551=ORIENTED_EDGE('',*,*,#16508,.T.);
#25552=ORIENTED_EDGE('',*,*,#16514,.T.);
#25553=ORIENTED_EDGE('',*,*,#16513,.T.);
#25554=ORIENTED_EDGE('',*,*,#16519,.T.);
#25555=ORIENTED_EDGE('',*,*,#16518,.T.);
#25556=ORIENTED_EDGE('',*,*,#16524,.T.);
#25557=ORIENTED_EDGE('',*,*,#16523,.T.);
#25558=ORIENTED_EDGE('',*,*,#16529,.T.);
#25559=ORIENTED_EDGE('',*,*,#16528,.T.);
#25560=ORIENTED_EDGE('',*,*,#16534,.T.);
#25561=ORIENTED_EDGE('',*,*,#16533,.T.);
#25562=ORIENTED_EDGE('',*,*,#16539,.T.);
#25563=ORIENTED_EDGE('',*,*,#16538,.T.);
#25564=ORIENTED_EDGE('',*,*,#16544,.T.);
#25565=ORIENTED_EDGE('',*,*,#16543,.T.);
#25566=ORIENTED_EDGE('',*,*,#16549,.T.);
#25567=ORIENTED_EDGE('',*,*,#16548,.T.);
#25568=ORIENTED_EDGE('',*,*,#16554,.T.);
#25569=ORIENTED_EDGE('',*,*,#16553,.T.);
#25570=ORIENTED_EDGE('',*,*,#16559,.T.);
#25571=ORIENTED_EDGE('',*,*,#16558,.T.);
#25572=ORIENTED_EDGE('',*,*,#16564,.T.);
#25573=ORIENTED_EDGE('',*,*,#16563,.T.);
#25574=ORIENTED_EDGE('',*,*,#16569,.T.);
#25575=ORIENTED_EDGE('',*,*,#16568,.T.);
#25576=ORIENTED_EDGE('',*,*,#16574,.T.);
#25577=ORIENTED_EDGE('',*,*,#16573,.T.);
#25578=ORIENTED_EDGE('',*,*,#16579,.T.);
#25579=ORIENTED_EDGE('',*,*,#16578,.T.);
#25580=ORIENTED_EDGE('',*,*,#17235,.T.);
#25581=ORIENTED_EDGE('',*,*,#17234,.T.);
#25582=ORIENTED_EDGE('',*,*,#17325,.T.);
#25583=ORIENTED_EDGE('',*,*,#17232,.F.);
#25584=ORIENTED_EDGE('',*,*,#17231,.F.);
#25585=ORIENTED_EDGE('',*,*,#16581,.F.);
#25586=ORIENTED_EDGE('',*,*,#16580,.F.);
#25587=ORIENTED_EDGE('',*,*,#16576,.F.);
#25588=ORIENTED_EDGE('',*,*,#16575,.F.);
#25589=ORIENTED_EDGE('',*,*,#16571,.F.);
#25590=ORIENTED_EDGE('',*,*,#16570,.F.);
#25591=ORIENTED_EDGE('',*,*,#16566,.F.);
#25592=ORIENTED_EDGE('',*,*,#16565,.F.);
#25593=ORIENTED_EDGE('',*,*,#16561,.F.);
#25594=ORIENTED_EDGE('',*,*,#16560,.F.);
#25595=ORIENTED_EDGE('',*,*,#16556,.F.);
#25596=ORIENTED_EDGE('',*,*,#16555,.F.);
#25597=ORIENTED_EDGE('',*,*,#16551,.F.);
#25598=ORIENTED_EDGE('',*,*,#16550,.F.);
#25599=ORIENTED_EDGE('',*,*,#16546,.F.);
#25600=ORIENTED_EDGE('',*,*,#16545,.F.);
#25601=ORIENTED_EDGE('',*,*,#16541,.F.);
#25602=ORIENTED_EDGE('',*,*,#16540,.F.);
#25603=ORIENTED_EDGE('',*,*,#16536,.F.);
#25604=ORIENTED_EDGE('',*,*,#16535,.F.);
#25605=ORIENTED_EDGE('',*,*,#16531,.F.);
#25606=ORIENTED_EDGE('',*,*,#16530,.F.);
#25607=ORIENTED_EDGE('',*,*,#16526,.F.);
#25608=ORIENTED_EDGE('',*,*,#16525,.F.);
#25609=ORIENTED_EDGE('',*,*,#16521,.F.);
#25610=ORIENTED_EDGE('',*,*,#16520,.F.);
#25611=ORIENTED_EDGE('',*,*,#16516,.F.);
#25612=ORIENTED_EDGE('',*,*,#16515,.F.);
#25613=ORIENTED_EDGE('',*,*,#16511,.F.);
#25614=ORIENTED_EDGE('',*,*,#16510,.F.);
#25615=ORIENTED_EDGE('',*,*,#16506,.F.);
#25616=ORIENTED_EDGE('',*,*,#16505,.F.);
#25617=ORIENTED_EDGE('',*,*,#16501,.F.);
#25618=ORIENTED_EDGE('',*,*,#16500,.F.);
#25619=ORIENTED_EDGE('',*,*,#16496,.F.);
#25620=ORIENTED_EDGE('',*,*,#16495,.F.);
#25621=ORIENTED_EDGE('',*,*,#16491,.F.);
#25622=ORIENTED_EDGE('',*,*,#16490,.F.);
#25623=ORIENTED_EDGE('',*,*,#16486,.F.);
#25624=ORIENTED_EDGE('',*,*,#16485,.F.);
#25625=ORIENTED_EDGE('',*,*,#16481,.F.);
#25626=ORIENTED_EDGE('',*,*,#16480,.F.);
#25627=ORIENTED_EDGE('',*,*,#16476,.F.);
#25628=ORIENTED_EDGE('',*,*,#16475,.F.);
#25629=ORIENTED_EDGE('',*,*,#16471,.F.);
#25630=ORIENTED_EDGE('',*,*,#16470,.F.);
#25631=ORIENTED_EDGE('',*,*,#16466,.F.);
#25632=ORIENTED_EDGE('',*,*,#16465,.F.);
#25633=ORIENTED_EDGE('',*,*,#16461,.F.);
#25634=ORIENTED_EDGE('',*,*,#16460,.F.);
#25635=ORIENTED_EDGE('',*,*,#16456,.F.);
#25636=ORIENTED_EDGE('',*,*,#16455,.F.);
#25637=ORIENTED_EDGE('',*,*,#16451,.F.);
#25638=ORIENTED_EDGE('',*,*,#16450,.F.);
#25639=ORIENTED_EDGE('',*,*,#17342,.T.);
#25640=ORIENTED_EDGE('',*,*,#16863,.T.);
#25641=ORIENTED_EDGE('',*,*,#16862,.T.);
#25642=ORIENTED_EDGE('',*,*,#16869,.T.);
#25643=ORIENTED_EDGE('',*,*,#16868,.T.);
#25644=ORIENTED_EDGE('',*,*,#16872,.T.);
#25645=ORIENTED_EDGE('',*,*,#16877,.T.);
#25646=ORIENTED_EDGE('',*,*,#16876,.T.);
#25647=ORIENTED_EDGE('',*,*,#16881,.T.);
#25648=ORIENTED_EDGE('',*,*,#16885,.T.);
#25649=ORIENTED_EDGE('',*,*,#16884,.T.);
#25650=ORIENTED_EDGE('',*,*,#16889,.T.);
#25651=ORIENTED_EDGE('',*,*,#16893,.T.);
#25652=ORIENTED_EDGE('',*,*,#16892,.T.);
#25653=ORIENTED_EDGE('',*,*,#16897,.T.);
#25654=ORIENTED_EDGE('',*,*,#16902,.T.);
#25655=ORIENTED_EDGE('',*,*,#16901,.T.);
#25656=ORIENTED_EDGE('',*,*,#16906,.T.);
#25657=ORIENTED_EDGE('',*,*,#16910,.T.);
#25658=ORIENTED_EDGE('',*,*,#16909,.T.);
#25659=ORIENTED_EDGE('',*,*,#16915,.T.);
#25660=ORIENTED_EDGE('',*,*,#16914,.T.);
#25661=ORIENTED_EDGE('',*,*,#16919,.T.);
#25662=ORIENTED_EDGE('',*,*,#16918,.T.);
#25663=ORIENTED_EDGE('',*,*,#16923,.T.);
#25664=ORIENTED_EDGE('',*,*,#16928,.T.);
#25665=ORIENTED_EDGE('',*,*,#16927,.T.);
#25666=ORIENTED_EDGE('',*,*,#16932,.T.);
#25667=ORIENTED_EDGE('',*,*,#16936,.T.);
#25668=ORIENTED_EDGE('',*,*,#16935,.T.);
#25669=ORIENTED_EDGE('',*,*,#16941,.T.);
#25670=ORIENTED_EDGE('',*,*,#16940,.T.);
#25671=ORIENTED_EDGE('',*,*,#16945,.T.);
#25672=ORIENTED_EDGE('',*,*,#16944,.T.);
#25673=ORIENTED_EDGE('',*,*,#16949,.T.);
#25674=ORIENTED_EDGE('',*,*,#16953,.T.);
#25675=ORIENTED_EDGE('',*,*,#16952,.T.);
#25676=ORIENTED_EDGE('',*,*,#16957,.T.);
#25677=ORIENTED_EDGE('',*,*,#16961,.T.);
#25678=ORIENTED_EDGE('',*,*,#16960,.T.);
#25679=ORIENTED_EDGE('',*,*,#16966,.T.);
#25680=ORIENTED_EDGE('',*,*,#16965,.T.);
#25681=ORIENTED_EDGE('',*,*,#16969,.T.);
#25682=ORIENTED_EDGE('',*,*,#16974,.T.);
#25683=ORIENTED_EDGE('',*,*,#16973,.T.);
#25684=ORIENTED_EDGE('',*,*,#17217,.T.);
#25685=ORIENTED_EDGE('',*,*,#17328,.T.);
#25686=ORIENTED_EDGE('',*,*,#17218,.T.);
#25687=ORIENTED_EDGE('',*,*,#16860,.T.);
#25688=ORIENTED_EDGE('',*,*,#16859,.T.);
#25689=ORIENTED_EDGE('',*,*,#16855,.T.);
#25690=ORIENTED_EDGE('',*,*,#16854,.T.);
#25691=ORIENTED_EDGE('',*,*,#16851,.T.);
#25692=ORIENTED_EDGE('',*,*,#16847,.T.);
#25693=ORIENTED_EDGE('',*,*,#16846,.T.);
#25694=ORIENTED_EDGE('',*,*,#16842,.T.);
#25695=ORIENTED_EDGE('',*,*,#16839,.T.);
#25696=ORIENTED_EDGE('',*,*,#16838,.T.);
#25697=ORIENTED_EDGE('',*,*,#16834,.T.);
#25698=ORIENTED_EDGE('',*,*,#16831,.T.);
#25699=ORIENTED_EDGE('',*,*,#16830,.T.);
#25700=ORIENTED_EDGE('',*,*,#16826,.T.);
#25701=ORIENTED_EDGE('',*,*,#16822,.T.);
#25702=ORIENTED_EDGE('',*,*,#16821,.T.);
#25703=ORIENTED_EDGE('',*,*,#16817,.T.);
#25704=ORIENTED_EDGE('',*,*,#16814,.T.);
#25705=ORIENTED_EDGE('',*,*,#16813,.T.);
#25706=ORIENTED_EDGE('',*,*,#16809,.T.);
#25707=ORIENTED_EDGE('',*,*,#16808,.T.);
#25708=ORIENTED_EDGE('',*,*,#16805,.T.);
#25709=ORIENTED_EDGE('',*,*,#16804,.T.);
#25710=ORIENTED_EDGE('',*,*,#16800,.T.);
#25711=ORIENTED_EDGE('',*,*,#16796,.T.);
#25712=ORIENTED_EDGE('',*,*,#16795,.T.);
#25713=ORIENTED_EDGE('',*,*,#16791,.T.);
#25714=ORIENTED_EDGE('',*,*,#16788,.T.);
#25715=ORIENTED_EDGE('',*,*,#16787,.T.);
#25716=ORIENTED_EDGE('',*,*,#16783,.T.);
#25717=ORIENTED_EDGE('',*,*,#16782,.T.);
#25718=ORIENTED_EDGE('',*,*,#16779,.T.);
#25719=ORIENTED_EDGE('',*,*,#16778,.T.);
#25720=ORIENTED_EDGE('',*,*,#16774,.T.);
#25721=ORIENTED_EDGE('',*,*,#16771,.T.);
#25722=ORIENTED_EDGE('',*,*,#16770,.T.);
#25723=ORIENTED_EDGE('',*,*,#16766,.T.);
#25724=ORIENTED_EDGE('',*,*,#16763,.T.);
#25725=ORIENTED_EDGE('',*,*,#16762,.T.);
#25726=ORIENTED_EDGE('',*,*,#16758,.T.);
#25727=ORIENTED_EDGE('',*,*,#16757,.T.);
#25728=ORIENTED_EDGE('',*,*,#16754,.T.);
#25729=ORIENTED_EDGE('',*,*,#16750,.T.);
#25730=ORIENTED_EDGE('',*,*,#16749,.T.);
#25731=ORIENTED_EDGE('',*,*,#17343,.T.);
#25732=ORIENTED_EDGE('',*,*,#16584,.T.);
#25733=ORIENTED_EDGE('',*,*,#16583,.T.);
#25734=ORIENTED_EDGE('',*,*,#16590,.T.);
#25735=ORIENTED_EDGE('',*,*,#16589,.T.);
#25736=ORIENTED_EDGE('',*,*,#16595,.T.);
#25737=ORIENTED_EDGE('',*,*,#16594,.T.);
#25738=ORIENTED_EDGE('',*,*,#16600,.T.);
#25739=ORIENTED_EDGE('',*,*,#16599,.T.);
#25740=ORIENTED_EDGE('',*,*,#16605,.T.);
#25741=ORIENTED_EDGE('',*,*,#16604,.T.);
#25742=ORIENTED_EDGE('',*,*,#16610,.T.);
#25743=ORIENTED_EDGE('',*,*,#16609,.T.);
#25744=ORIENTED_EDGE('',*,*,#16615,.T.);
#25745=ORIENTED_EDGE('',*,*,#16614,.T.);
#25746=ORIENTED_EDGE('',*,*,#16620,.T.);
#25747=ORIENTED_EDGE('',*,*,#16619,.T.);
#25748=ORIENTED_EDGE('',*,*,#16625,.T.);
#25749=ORIENTED_EDGE('',*,*,#16624,.T.);
#25750=ORIENTED_EDGE('',*,*,#16630,.T.);
#25751=ORIENTED_EDGE('',*,*,#16629,.T.);
#25752=ORIENTED_EDGE('',*,*,#16635,.T.);
#25753=ORIENTED_EDGE('',*,*,#16634,.T.);
#25754=ORIENTED_EDGE('',*,*,#16640,.T.);
#25755=ORIENTED_EDGE('',*,*,#16639,.T.);
#25756=ORIENTED_EDGE('',*,*,#16645,.T.);
#25757=ORIENTED_EDGE('',*,*,#16644,.T.);
#25758=ORIENTED_EDGE('',*,*,#16650,.T.);
#25759=ORIENTED_EDGE('',*,*,#16649,.T.);
#25760=ORIENTED_EDGE('',*,*,#16655,.T.);
#25761=ORIENTED_EDGE('',*,*,#16654,.T.);
#25762=ORIENTED_EDGE('',*,*,#16660,.T.);
#25763=ORIENTED_EDGE('',*,*,#16659,.T.);
#25764=ORIENTED_EDGE('',*,*,#16665,.T.);
#25765=ORIENTED_EDGE('',*,*,#16664,.T.);
#25766=ORIENTED_EDGE('',*,*,#16670,.T.);
#25767=ORIENTED_EDGE('',*,*,#16669,.T.);
#25768=ORIENTED_EDGE('',*,*,#16675,.T.);
#25769=ORIENTED_EDGE('',*,*,#16674,.T.);
#25770=ORIENTED_EDGE('',*,*,#16680,.T.);
#25771=ORIENTED_EDGE('',*,*,#16679,.T.);
#25772=ORIENTED_EDGE('',*,*,#16685,.T.);
#25773=ORIENTED_EDGE('',*,*,#16684,.T.);
#25774=ORIENTED_EDGE('',*,*,#16690,.T.);
#25775=ORIENTED_EDGE('',*,*,#16689,.T.);
#25776=ORIENTED_EDGE('',*,*,#16695,.T.);
#25777=ORIENTED_EDGE('',*,*,#16694,.T.);
#25778=ORIENTED_EDGE('',*,*,#16700,.T.);
#25779=ORIENTED_EDGE('',*,*,#16699,.T.);
#25780=ORIENTED_EDGE('',*,*,#16705,.T.);
#25781=ORIENTED_EDGE('',*,*,#16704,.T.);
#25782=ORIENTED_EDGE('',*,*,#16710,.T.);
#25783=ORIENTED_EDGE('',*,*,#16709,.T.);
#25784=ORIENTED_EDGE('',*,*,#16715,.T.);
#25785=ORIENTED_EDGE('',*,*,#16714,.T.);
#25786=ORIENTED_EDGE('',*,*,#17230,.T.);
#25787=ORIENTED_EDGE('',*,*,#17229,.T.);
#25788=ORIENTED_EDGE('',*,*,#17327,.T.);
#25789=ORIENTED_EDGE('',*,*,#17227,.F.);
#25790=ORIENTED_EDGE('',*,*,#17226,.F.);
#25791=ORIENTED_EDGE('',*,*,#16717,.F.);
#25792=ORIENTED_EDGE('',*,*,#16716,.F.);
#25793=ORIENTED_EDGE('',*,*,#16712,.F.);
#25794=ORIENTED_EDGE('',*,*,#16711,.F.);
#25795=ORIENTED_EDGE('',*,*,#16707,.F.);
#25796=ORIENTED_EDGE('',*,*,#16706,.F.);
#25797=ORIENTED_EDGE('',*,*,#16702,.F.);
#25798=ORIENTED_EDGE('',*,*,#16701,.F.);
#25799=ORIENTED_EDGE('',*,*,#16697,.F.);
#25800=ORIENTED_EDGE('',*,*,#16696,.F.);
#25801=ORIENTED_EDGE('',*,*,#16692,.F.);
#25802=ORIENTED_EDGE('',*,*,#16691,.F.);
#25803=ORIENTED_EDGE('',*,*,#16687,.F.);
#25804=ORIENTED_EDGE('',*,*,#16686,.F.);
#25805=ORIENTED_EDGE('',*,*,#16682,.F.);
#25806=ORIENTED_EDGE('',*,*,#16681,.F.);
#25807=ORIENTED_EDGE('',*,*,#16677,.F.);
#25808=ORIENTED_EDGE('',*,*,#16676,.F.);
#25809=ORIENTED_EDGE('',*,*,#16672,.F.);
#25810=ORIENTED_EDGE('',*,*,#16671,.F.);
#25811=ORIENTED_EDGE('',*,*,#16667,.F.);
#25812=ORIENTED_EDGE('',*,*,#16666,.F.);
#25813=ORIENTED_EDGE('',*,*,#16662,.F.);
#25814=ORIENTED_EDGE('',*,*,#16661,.F.);
#25815=ORIENTED_EDGE('',*,*,#16657,.F.);
#25816=ORIENTED_EDGE('',*,*,#16656,.F.);
#25817=ORIENTED_EDGE('',*,*,#16652,.F.);
#25818=ORIENTED_EDGE('',*,*,#16651,.F.);
#25819=ORIENTED_EDGE('',*,*,#16647,.F.);
#25820=ORIENTED_EDGE('',*,*,#16646,.F.);
#25821=ORIENTED_EDGE('',*,*,#16642,.F.);
#25822=ORIENTED_EDGE('',*,*,#16641,.F.);
#25823=ORIENTED_EDGE('',*,*,#16637,.F.);
#25824=ORIENTED_EDGE('',*,*,#16636,.F.);
#25825=ORIENTED_EDGE('',*,*,#16632,.F.);
#25826=ORIENTED_EDGE('',*,*,#16631,.F.);
#25827=ORIENTED_EDGE('',*,*,#16627,.F.);
#25828=ORIENTED_EDGE('',*,*,#16626,.F.);
#25829=ORIENTED_EDGE('',*,*,#16622,.F.);
#25830=ORIENTED_EDGE('',*,*,#16621,.F.);
#25831=ORIENTED_EDGE('',*,*,#16617,.F.);
#25832=ORIENTED_EDGE('',*,*,#16616,.F.);
#25833=ORIENTED_EDGE('',*,*,#16612,.F.);
#25834=ORIENTED_EDGE('',*,*,#16611,.F.);
#25835=ORIENTED_EDGE('',*,*,#16607,.F.);
#25836=ORIENTED_EDGE('',*,*,#16606,.F.);
#25837=ORIENTED_EDGE('',*,*,#16602,.F.);
#25838=ORIENTED_EDGE('',*,*,#16601,.F.);
#25839=ORIENTED_EDGE('',*,*,#16597,.F.);
#25840=ORIENTED_EDGE('',*,*,#16596,.F.);
#25841=ORIENTED_EDGE('',*,*,#16592,.F.);
#25842=ORIENTED_EDGE('',*,*,#16591,.F.);
#25843=ORIENTED_EDGE('',*,*,#16587,.F.);
#25844=ORIENTED_EDGE('',*,*,#16586,.F.);
#25845=ORIENTED_EDGE('',*,*,#17344,.T.);
#25846=ORIENTED_EDGE('',*,*,#16747,.T.);
#25847=ORIENTED_EDGE('',*,*,#16746,.T.);
#25848=ORIENTED_EDGE('',*,*,#16753,.T.);
#25849=ORIENTED_EDGE('',*,*,#16752,.T.);
#25850=ORIENTED_EDGE('',*,*,#16756,.T.);
#25851=ORIENTED_EDGE('',*,*,#16761,.T.);
#25852=ORIENTED_EDGE('',*,*,#16760,.T.);
#25853=ORIENTED_EDGE('',*,*,#16765,.T.);
#25854=ORIENTED_EDGE('',*,*,#16769,.T.);
#25855=ORIENTED_EDGE('',*,*,#16768,.T.);
#25856=ORIENTED_EDGE('',*,*,#16773,.T.);
#25857=ORIENTED_EDGE('',*,*,#16777,.T.);
#25858=ORIENTED_EDGE('',*,*,#16776,.T.);
#25859=ORIENTED_EDGE('',*,*,#16781,.T.);
#25860=ORIENTED_EDGE('',*,*,#16786,.T.);
#25861=ORIENTED_EDGE('',*,*,#16785,.T.);
#25862=ORIENTED_EDGE('',*,*,#16790,.T.);
#25863=ORIENTED_EDGE('',*,*,#16794,.T.);
#25864=ORIENTED_EDGE('',*,*,#16793,.T.);
#25865=ORIENTED_EDGE('',*,*,#16799,.T.);
#25866=ORIENTED_EDGE('',*,*,#16798,.T.);
#25867=ORIENTED_EDGE('',*,*,#16803,.T.);
#25868=ORIENTED_EDGE('',*,*,#16802,.T.);
#25869=ORIENTED_EDGE('',*,*,#16807,.T.);
#25870=ORIENTED_EDGE('',*,*,#16812,.T.);
#25871=ORIENTED_EDGE('',*,*,#16811,.T.);
#25872=ORIENTED_EDGE('',*,*,#16816,.T.);
#25873=ORIENTED_EDGE('',*,*,#16820,.T.);
#25874=ORIENTED_EDGE('',*,*,#16819,.T.);
#25875=ORIENTED_EDGE('',*,*,#16825,.T.);
#25876=ORIENTED_EDGE('',*,*,#16824,.T.);
#25877=ORIENTED_EDGE('',*,*,#16829,.T.);
#25878=ORIENTED_EDGE('',*,*,#16828,.T.);
#25879=ORIENTED_EDGE('',*,*,#16833,.T.);
#25880=ORIENTED_EDGE('',*,*,#16837,.T.);
#25881=ORIENTED_EDGE('',*,*,#16836,.T.);
#25882=ORIENTED_EDGE('',*,*,#16841,.T.);
#25883=ORIENTED_EDGE('',*,*,#16845,.T.);
#25884=ORIENTED_EDGE('',*,*,#16844,.T.);
#25885=ORIENTED_EDGE('',*,*,#16850,.T.);
#25886=ORIENTED_EDGE('',*,*,#16849,.T.);
#25887=ORIENTED_EDGE('',*,*,#16853,.T.);
#25888=ORIENTED_EDGE('',*,*,#16858,.T.);
#25889=ORIENTED_EDGE('',*,*,#16857,.T.);
#25890=ORIENTED_EDGE('',*,*,#17220,.T.);
#25891=ORIENTED_EDGE('',*,*,#17345,.T.);
#25892=ORIENTED_EDGE('',*,*,#17346,.T.);
#25893=ORIENTED_EDGE('',*,*,#17347,.T.);
#25894=ORIENTED_EDGE('',*,*,#17348,.F.);
#25895=ORIENTED_EDGE('',*,*,#17349,.T.);
#25896=ORIENTED_EDGE('',*,*,#17350,.T.);
#25897=ORIENTED_EDGE('',*,*,#17351,.T.);
#25898=ORIENTED_EDGE('',*,*,#17346,.F.);
#25899=ORIENTED_EDGE('',*,*,#17352,.T.);
#25900=ORIENTED_EDGE('',*,*,#17353,.T.);
#25901=ORIENTED_EDGE('',*,*,#17354,.T.);
#25902=ORIENTED_EDGE('',*,*,#17350,.F.);
#25903=ORIENTED_EDGE('',*,*,#17355,.T.);
#25904=ORIENTED_EDGE('',*,*,#17356,.T.);
#25905=ORIENTED_EDGE('',*,*,#17357,.T.);
#25906=ORIENTED_EDGE('',*,*,#17353,.F.);
#25907=ORIENTED_EDGE('',*,*,#17358,.T.);
#25908=ORIENTED_EDGE('',*,*,#17359,.T.);
#25909=ORIENTED_EDGE('',*,*,#17360,.T.);
#25910=ORIENTED_EDGE('',*,*,#17356,.F.);
#25911=ORIENTED_EDGE('',*,*,#17361,.T.);
#25912=ORIENTED_EDGE('',*,*,#17362,.T.);
#25913=ORIENTED_EDGE('',*,*,#17363,.T.);
#25914=ORIENTED_EDGE('',*,*,#17359,.F.);
#25915=ORIENTED_EDGE('',*,*,#17364,.T.);
#25916=ORIENTED_EDGE('',*,*,#17348,.T.);
#25917=ORIENTED_EDGE('',*,*,#17365,.T.);
#25918=ORIENTED_EDGE('',*,*,#17362,.F.);
#25919=ORIENTED_EDGE('',*,*,#17366,.T.);
#25920=ORIENTED_EDGE('',*,*,#17367,.T.);
#25921=ORIENTED_EDGE('',*,*,#17368,.T.);
#25922=ORIENTED_EDGE('',*,*,#17367,.F.);
#25923=ORIENTED_EDGE('',*,*,#17368,.F.);
#25924=ORIENTED_EDGE('',*,*,#17365,.F.);
#25925=ORIENTED_EDGE('',*,*,#17347,.F.);
#25926=ORIENTED_EDGE('',*,*,#17351,.F.);
#25927=ORIENTED_EDGE('',*,*,#17354,.F.);
#25928=ORIENTED_EDGE('',*,*,#17357,.F.);
#25929=ORIENTED_EDGE('',*,*,#17360,.F.);
#25930=ORIENTED_EDGE('',*,*,#17363,.F.);
#25931=ORIENTED_EDGE('',*,*,#17369,.T.);
#25932=ORIENTED_EDGE('',*,*,#17370,.T.);
#25933=ORIENTED_EDGE('',*,*,#17371,.T.);
#25934=ORIENTED_EDGE('',*,*,#17372,.F.);
#25935=ORIENTED_EDGE('',*,*,#17373,.T.);
#25936=ORIENTED_EDGE('',*,*,#17374,.T.);
#25937=ORIENTED_EDGE('',*,*,#17375,.T.);
#25938=ORIENTED_EDGE('',*,*,#17370,.F.);
#25939=ORIENTED_EDGE('',*,*,#17376,.T.);
#25940=ORIENTED_EDGE('',*,*,#17377,.T.);
#25941=ORIENTED_EDGE('',*,*,#17378,.T.);
#25942=ORIENTED_EDGE('',*,*,#17374,.F.);
#25943=ORIENTED_EDGE('',*,*,#17379,.T.);
#25944=ORIENTED_EDGE('',*,*,#17309,.T.);
#25945=ORIENTED_EDGE('',*,*,#17380,.T.);
#25946=ORIENTED_EDGE('',*,*,#17377,.F.);
#25947=ORIENTED_EDGE('',*,*,#17381,.T.);
#25948=ORIENTED_EDGE('',*,*,#17372,.T.);
#25949=ORIENTED_EDGE('',*,*,#17382,.T.);
#25950=ORIENTED_EDGE('',*,*,#17307,.T.);
#25951=ORIENTED_EDGE('',*,*,#17382,.F.);
#25952=ORIENTED_EDGE('',*,*,#17371,.F.);
#25953=ORIENTED_EDGE('',*,*,#17375,.F.);
#25954=ORIENTED_EDGE('',*,*,#17378,.F.);
#25955=ORIENTED_EDGE('',*,*,#17380,.F.);
#25956=ORIENTED_EDGE('',*,*,#17308,.T.);
#25957=ORIENTED_EDGE('',*,*,#17336,.F.);
#25958=ORIENTED_EDGE('',*,*,#16157,.F.);
#25959=ORIENTED_EDGE('',*,*,#17334,.F.);
#25960=ORIENTED_EDGE('',*,*,#17224,.T.);
#25961=ORIENTED_EDGE('',*,*,#17383,.T.);
#25962=ORIENTED_EDGE('',*,*,#17384,.T.);
#25963=ORIENTED_EDGE('',*,*,#17385,.T.);
#25964=ORIENTED_EDGE('',*,*,#17386,.T.);
#25965=ORIENTED_EDGE('',*,*,#17387,.T.);
#25966=ORIENTED_EDGE('',*,*,#17388,.F.);
#25967=ORIENTED_EDGE('',*,*,#17389,.T.);
#25968=ORIENTED_EDGE('',*,*,#17390,.T.);
#25969=ORIENTED_EDGE('',*,*,#17391,.T.);
#25970=ORIENTED_EDGE('',*,*,#17386,.F.);
#25971=ORIENTED_EDGE('',*,*,#17392,.T.);
#25972=ORIENTED_EDGE('',*,*,#17393,.T.);
#25973=ORIENTED_EDGE('',*,*,#17394,.T.);
#25974=ORIENTED_EDGE('',*,*,#17390,.F.);
#25975=ORIENTED_EDGE('',*,*,#17395,.T.);
#25976=ORIENTED_EDGE('',*,*,#17396,.T.);
#25977=ORIENTED_EDGE('',*,*,#17397,.T.);
#25978=ORIENTED_EDGE('',*,*,#17393,.F.);
#25979=ORIENTED_EDGE('',*,*,#17398,.T.);
#25980=ORIENTED_EDGE('',*,*,#17399,.T.);
#25981=ORIENTED_EDGE('',*,*,#17400,.T.);
#25982=ORIENTED_EDGE('',*,*,#17396,.F.);
#25983=ORIENTED_EDGE('',*,*,#17401,.T.);
#25984=ORIENTED_EDGE('',*,*,#17402,.T.);
#25985=ORIENTED_EDGE('',*,*,#17403,.T.);
#25986=ORIENTED_EDGE('',*,*,#17399,.F.);
#25987=ORIENTED_EDGE('',*,*,#17404,.T.);
#25988=ORIENTED_EDGE('',*,*,#17388,.T.);
#25989=ORIENTED_EDGE('',*,*,#17405,.T.);
#25990=ORIENTED_EDGE('',*,*,#17402,.F.);
#25991=ORIENTED_EDGE('',*,*,#17406,.T.);
#25992=ORIENTED_EDGE('',*,*,#17407,.T.);
#25993=ORIENTED_EDGE('',*,*,#17408,.T.);
#25994=ORIENTED_EDGE('',*,*,#17407,.F.);
#25995=ORIENTED_EDGE('',*,*,#17408,.F.);
#25996=ORIENTED_EDGE('',*,*,#17405,.F.);
#25997=ORIENTED_EDGE('',*,*,#17387,.F.);
#25998=ORIENTED_EDGE('',*,*,#17391,.F.);
#25999=ORIENTED_EDGE('',*,*,#17394,.F.);
#26000=ORIENTED_EDGE('',*,*,#17397,.F.);
#26001=ORIENTED_EDGE('',*,*,#17400,.F.);
#26002=ORIENTED_EDGE('',*,*,#17403,.F.);
#26003=ORIENTED_EDGE('',*,*,#17385,.F.);
#26004=ORIENTED_EDGE('',*,*,#17404,.F.);
#26005=ORIENTED_EDGE('',*,*,#17401,.F.);
#26006=ORIENTED_EDGE('',*,*,#17398,.F.);
#26007=ORIENTED_EDGE('',*,*,#17395,.F.);
#26008=ORIENTED_EDGE('',*,*,#17392,.F.);
#26009=ORIENTED_EDGE('',*,*,#17389,.F.);
#26010=ORIENTED_EDGE('',*,*,#17345,.F.);
#26011=ORIENTED_EDGE('',*,*,#17364,.F.);
#26012=ORIENTED_EDGE('',*,*,#17361,.F.);
#26013=ORIENTED_EDGE('',*,*,#17358,.F.);
#26014=ORIENTED_EDGE('',*,*,#17355,.F.);
#26015=ORIENTED_EDGE('',*,*,#17352,.F.);
#26016=ORIENTED_EDGE('',*,*,#17349,.F.);
#26017=ORIENTED_EDGE('',*,*,#17383,.F.);
#26018=ORIENTED_EDGE('',*,*,#17409,.T.);
#26019=ORIENTED_EDGE('',*,*,#17410,.T.);
#26020=ORIENTED_EDGE('',*,*,#17409,.F.);
#26021=ORIENTED_EDGE('',*,*,#17410,.F.);
#26022=ORIENTED_EDGE('',*,*,#16720,.F.);
#26023=ORIENTED_EDGE('',*,*,#17333,.F.);
#26024=ORIENTED_EDGE('',*,*,#17248,.F.);
#26025=ORIENTED_EDGE('',*,*,#17335,.F.);
#26026=ORIENTED_EDGE('',*,*,#16723,.F.);
#26027=ORIENTED_EDGE('',*,*,#17384,.F.);
#26028=ORIENTED_EDGE('',*,*,#17411,.T.);
#26029=ORIENTED_EDGE('',*,*,#17412,.T.);
#26030=ORIENTED_EDGE('',*,*,#17411,.F.);
#26031=ORIENTED_EDGE('',*,*,#17412,.F.);
#26032=ORIENTED_EDGE('',*,*,#17413,.T.);
#26033=ORIENTED_EDGE('',*,*,#17414,.T.);
#26034=ORIENTED_EDGE('',*,*,#17415,.F.);
#26035=ORIENTED_EDGE('',*,*,#17416,.F.);
#26036=ORIENTED_EDGE('',*,*,#17417,.T.);
#26037=ORIENTED_EDGE('',*,*,#17416,.T.);
#26038=ORIENTED_EDGE('',*,*,#17418,.F.);
#26039=ORIENTED_EDGE('',*,*,#17419,.F.);
#26040=ORIENTED_EDGE('',*,*,#17420,.T.);
#26041=ORIENTED_EDGE('',*,*,#17419,.T.);
#26042=ORIENTED_EDGE('',*,*,#17421,.F.);
#26043=ORIENTED_EDGE('',*,*,#17422,.F.);
#26044=ORIENTED_EDGE('',*,*,#17423,.T.);
#26045=ORIENTED_EDGE('',*,*,#17422,.T.);
#26046=ORIENTED_EDGE('',*,*,#17424,.F.);
#26047=ORIENTED_EDGE('',*,*,#17299,.T.);
#26048=ORIENTED_EDGE('',*,*,#17425,.T.);
#26049=ORIENTED_EDGE('',*,*,#17301,.T.);
#26050=ORIENTED_EDGE('',*,*,#17426,.F.);
#26051=ORIENTED_EDGE('',*,*,#17414,.F.);
#26052=ORIENTED_EDGE('',*,*,#17426,.T.);
#26053=ORIENTED_EDGE('',*,*,#17300,.T.);
#26054=ORIENTED_EDGE('',*,*,#17424,.T.);
#26055=ORIENTED_EDGE('',*,*,#17421,.T.);
#26056=ORIENTED_EDGE('',*,*,#17418,.T.);
#26057=ORIENTED_EDGE('',*,*,#17415,.T.);
#26058=ORIENTED_EDGE('',*,*,#17332,.F.);
#26059=ORIENTED_EDGE('',*,*,#16138,.F.);
#26060=ORIENTED_EDGE('',*,*,#17330,.F.);
#26061=ORIENTED_EDGE('',*,*,#16733,.T.);
#26062=ORIENTED_EDGE('',*,*,#17427,.T.);
#26063=ORIENTED_EDGE('',*,*,#17428,.T.);
#26064=ORIENTED_EDGE('',*,*,#17429,.T.);
#26065=ORIENTED_EDGE('',*,*,#17430,.T.);
#26066=ORIENTED_EDGE('',*,*,#17431,.F.);
#26067=ORIENTED_EDGE('',*,*,#17432,.F.);
#26068=ORIENTED_EDGE('',*,*,#17433,.T.);
#26069=ORIENTED_EDGE('',*,*,#17432,.T.);
#26070=ORIENTED_EDGE('',*,*,#17434,.F.);
#26071=ORIENTED_EDGE('',*,*,#17435,.F.);
#26072=ORIENTED_EDGE('',*,*,#17436,.T.);
#26073=ORIENTED_EDGE('',*,*,#17435,.T.);
#26074=ORIENTED_EDGE('',*,*,#17437,.F.);
#26075=ORIENTED_EDGE('',*,*,#17438,.F.);
#26076=ORIENTED_EDGE('',*,*,#17439,.T.);
#26077=ORIENTED_EDGE('',*,*,#17438,.T.);
#26078=ORIENTED_EDGE('',*,*,#17440,.F.);
#26079=ORIENTED_EDGE('',*,*,#17441,.F.);
#26080=ORIENTED_EDGE('',*,*,#17442,.T.);
#26081=ORIENTED_EDGE('',*,*,#17441,.T.);
#26082=ORIENTED_EDGE('',*,*,#17443,.F.);
#26083=ORIENTED_EDGE('',*,*,#17444,.F.);
#26084=ORIENTED_EDGE('',*,*,#17445,.T.);
#26085=ORIENTED_EDGE('',*,*,#17444,.T.);
#26086=ORIENTED_EDGE('',*,*,#17446,.F.);
#26087=ORIENTED_EDGE('',*,*,#17447,.F.);
#26088=ORIENTED_EDGE('',*,*,#17448,.T.);
#26089=ORIENTED_EDGE('',*,*,#17447,.T.);
#26090=ORIENTED_EDGE('',*,*,#17449,.F.);
#26091=ORIENTED_EDGE('',*,*,#17430,.F.);
#26092=ORIENTED_EDGE('',*,*,#17450,.F.);
#26093=ORIENTED_EDGE('',*,*,#17451,.T.);
#26094=ORIENTED_EDGE('',*,*,#17452,.T.);
#26095=ORIENTED_EDGE('',*,*,#17451,.F.);
#26096=ORIENTED_EDGE('',*,*,#17450,.T.);
#26097=ORIENTED_EDGE('',*,*,#17449,.T.);
#26098=ORIENTED_EDGE('',*,*,#17446,.T.);
#26099=ORIENTED_EDGE('',*,*,#17443,.T.);
#26100=ORIENTED_EDGE('',*,*,#17440,.T.);
#26101=ORIENTED_EDGE('',*,*,#17437,.T.);
#26102=ORIENTED_EDGE('',*,*,#17434,.T.);
#26103=ORIENTED_EDGE('',*,*,#17431,.T.);
#26104=ORIENTED_EDGE('',*,*,#17453,.T.);
#26105=ORIENTED_EDGE('',*,*,#17454,.T.);
#26106=ORIENTED_EDGE('',*,*,#17455,.F.);
#26107=ORIENTED_EDGE('',*,*,#17456,.F.);
#26108=ORIENTED_EDGE('',*,*,#17457,.T.);
#26109=ORIENTED_EDGE('',*,*,#17456,.T.);
#26110=ORIENTED_EDGE('',*,*,#17458,.F.);
#26111=ORIENTED_EDGE('',*,*,#17459,.F.);
#26112=ORIENTED_EDGE('',*,*,#17460,.T.);
#26113=ORIENTED_EDGE('',*,*,#17459,.T.);
#26114=ORIENTED_EDGE('',*,*,#17461,.F.);
#26115=ORIENTED_EDGE('',*,*,#17462,.F.);
#26116=ORIENTED_EDGE('',*,*,#17463,.T.);
#26117=ORIENTED_EDGE('',*,*,#17462,.T.);
#26118=ORIENTED_EDGE('',*,*,#17464,.F.);
#26119=ORIENTED_EDGE('',*,*,#17465,.F.);
#26120=ORIENTED_EDGE('',*,*,#17466,.T.);
#26121=ORIENTED_EDGE('',*,*,#17465,.T.);
#26122=ORIENTED_EDGE('',*,*,#17467,.F.);
#26123=ORIENTED_EDGE('',*,*,#17468,.F.);
#26124=ORIENTED_EDGE('',*,*,#17469,.T.);
#26125=ORIENTED_EDGE('',*,*,#17468,.T.);
#26126=ORIENTED_EDGE('',*,*,#17470,.F.);
#26127=ORIENTED_EDGE('',*,*,#17471,.F.);
#26128=ORIENTED_EDGE('',*,*,#17472,.T.);
#26129=ORIENTED_EDGE('',*,*,#17471,.T.);
#26130=ORIENTED_EDGE('',*,*,#17473,.F.);
#26131=ORIENTED_EDGE('',*,*,#17454,.F.);
#26132=ORIENTED_EDGE('',*,*,#17474,.F.);
#26133=ORIENTED_EDGE('',*,*,#17475,.T.);
#26134=ORIENTED_EDGE('',*,*,#17476,.T.);
#26135=ORIENTED_EDGE('',*,*,#17475,.F.);
#26136=ORIENTED_EDGE('',*,*,#17474,.T.);
#26137=ORIENTED_EDGE('',*,*,#17473,.T.);
#26138=ORIENTED_EDGE('',*,*,#17470,.T.);
#26139=ORIENTED_EDGE('',*,*,#17467,.T.);
#26140=ORIENTED_EDGE('',*,*,#17464,.T.);
#26141=ORIENTED_EDGE('',*,*,#17461,.T.);
#26142=ORIENTED_EDGE('',*,*,#17458,.T.);
#26143=ORIENTED_EDGE('',*,*,#17455,.T.);
#26144=ORIENTED_EDGE('',*,*,#17453,.F.);
#26145=ORIENTED_EDGE('',*,*,#17457,.F.);
#26146=ORIENTED_EDGE('',*,*,#17460,.F.);
#26147=ORIENTED_EDGE('',*,*,#17463,.F.);
#26148=ORIENTED_EDGE('',*,*,#17466,.F.);
#26149=ORIENTED_EDGE('',*,*,#17469,.F.);
#26150=ORIENTED_EDGE('',*,*,#17472,.F.);
#26151=ORIENTED_EDGE('',*,*,#17429,.F.);
#26152=ORIENTED_EDGE('',*,*,#17433,.F.);
#26153=ORIENTED_EDGE('',*,*,#17436,.F.);
#26154=ORIENTED_EDGE('',*,*,#17439,.F.);
#26155=ORIENTED_EDGE('',*,*,#17442,.F.);
#26156=ORIENTED_EDGE('',*,*,#17445,.F.);
#26157=ORIENTED_EDGE('',*,*,#17448,.F.);
#26158=ORIENTED_EDGE('',*,*,#17423,.F.);
#26159=ORIENTED_EDGE('',*,*,#17298,.T.);
#26160=ORIENTED_EDGE('',*,*,#17477,.F.);
#26161=ORIENTED_EDGE('',*,*,#17478,.T.);
#26162=ORIENTED_EDGE('',*,*,#17479,.T.);
#26163=ORIENTED_EDGE('',*,*,#17302,.T.);
#26164=ORIENTED_EDGE('',*,*,#17425,.F.);
#26165=ORIENTED_EDGE('',*,*,#17413,.F.);
#26166=ORIENTED_EDGE('',*,*,#17417,.F.);
#26167=ORIENTED_EDGE('',*,*,#17420,.F.);
#26168=ORIENTED_EDGE('',*,*,#17476,.F.);
#26169=ORIENTED_EDGE('',*,*,#17452,.F.);
#26170=ORIENTED_EDGE('',*,*,#16742,.T.);
#26171=ORIENTED_EDGE('',*,*,#17222,.T.);
#26172=ORIENTED_EDGE('',*,*,#17329,.F.);
#26173=ORIENTED_EDGE('',*,*,#17253,.F.);
#26174=ORIENTED_EDGE('',*,*,#17331,.F.);
#26175=ORIENTED_EDGE('',*,*,#17480,.F.);
#26176=ORIENTED_EDGE('',*,*,#17481,.T.);
#26177=ORIENTED_EDGE('',*,*,#17428,.F.);
#26178=ORIENTED_EDGE('',*,*,#17481,.F.);
#26179=ORIENTED_EDGE('',*,*,#17480,.T.);
#26180=ORIENTED_EDGE('',*,*,#17482,.F.);
#26181=ORIENTED_EDGE('',*,*,#17483,.T.);
#26182=ORIENTED_EDGE('',*,*,#17427,.F.);
#26183=ORIENTED_EDGE('',*,*,#17483,.F.);
#26184=ORIENTED_EDGE('',*,*,#17482,.T.);
#26185=ORIENTED_EDGE('',*,*,#17484,.F.);
#26186=ORIENTED_EDGE('',*,*,#17485,.T.);
#26187=ORIENTED_EDGE('',*,*,#17319,.T.);
#26188=ORIENTED_EDGE('',*,*,#17485,.F.);
#26189=ORIENTED_EDGE('',*,*,#17484,.T.);
#26190=ORIENTED_EDGE('',*,*,#17486,.F.);
#26191=ORIENTED_EDGE('',*,*,#17487,.T.);
#26192=ORIENTED_EDGE('',*,*,#17320,.T.);
#26193=ORIENTED_EDGE('',*,*,#17487,.F.);
#26194=ORIENTED_EDGE('',*,*,#17486,.T.);
#26195=ORIENTED_EDGE('',*,*,#17274,.F.);
#26196=ORIENTED_EDGE('',*,*,#17289,.F.);
#26197=ORIENTED_EDGE('',*,*,#17488,.T.);
#26198=ORIENTED_EDGE('',*,*,#17489,.T.);
#26199=ORIENTED_EDGE('',*,*,#17275,.F.);
#26200=ORIENTED_EDGE('',*,*,#17489,.F.);
#26201=ORIENTED_EDGE('',*,*,#17490,.T.);
#26202=ORIENTED_EDGE('',*,*,#17284,.T.);
#26203=ORIENTED_EDGE('',*,*,#17491,.F.);
#26204=ORIENTED_EDGE('',*,*,#17492,.T.);
#26205=ORIENTED_EDGE('',*,*,#17291,.T.);
#26206=ORIENTED_EDGE('',*,*,#17286,.F.);
#26207=ORIENTED_EDGE('',*,*,#17493,.T.);
#26208=ORIENTED_EDGE('',*,*,#17494,.T.);
#26209=ORIENTED_EDGE('',*,*,#17292,.T.);
#26210=ORIENTED_EDGE('',*,*,#17492,.F.);
#26211=ORIENTED_EDGE('',*,*,#17495,.T.);
#26212=ORIENTED_EDGE('',*,*,#17496,.T.);
#26213=ORIENTED_EDGE('',*,*,#17293,.T.);
#26214=ORIENTED_EDGE('',*,*,#17494,.F.);
#26215=ORIENTED_EDGE('',*,*,#17497,.T.);
#26216=ORIENTED_EDGE('',*,*,#17498,.T.);
#26217=ORIENTED_EDGE('',*,*,#17294,.T.);
#26218=ORIENTED_EDGE('',*,*,#17496,.F.);
#26219=ORIENTED_EDGE('',*,*,#17499,.T.);
#26220=ORIENTED_EDGE('',*,*,#17500,.T.);
#26221=ORIENTED_EDGE('',*,*,#17295,.T.);
#26222=ORIENTED_EDGE('',*,*,#17498,.F.);
#26223=ORIENTED_EDGE('',*,*,#17501,.T.);
#26224=ORIENTED_EDGE('',*,*,#17502,.T.);
#26225=ORIENTED_EDGE('',*,*,#17296,.T.);
#26226=ORIENTED_EDGE('',*,*,#17500,.F.);
#26227=ORIENTED_EDGE('',*,*,#17503,.T.);
#26228=ORIENTED_EDGE('',*,*,#17477,.T.);
#26229=ORIENTED_EDGE('',*,*,#17297,.T.);
#26230=ORIENTED_EDGE('',*,*,#17502,.F.);
#26231=ORIENTED_EDGE('',*,*,#17504,.T.);
#26232=ORIENTED_EDGE('',*,*,#17505,.T.);
#26233=ORIENTED_EDGE('',*,*,#17303,.T.);
#26234=ORIENTED_EDGE('',*,*,#17479,.F.);
#26235=ORIENTED_EDGE('',*,*,#17506,.T.);
#26236=ORIENTED_EDGE('',*,*,#17507,.T.);
#26237=ORIENTED_EDGE('',*,*,#17304,.T.);
#26238=ORIENTED_EDGE('',*,*,#17505,.F.);
#26239=ORIENTED_EDGE('',*,*,#17508,.T.);
#26240=ORIENTED_EDGE('',*,*,#17509,.T.);
#26241=ORIENTED_EDGE('',*,*,#17305,.T.);
#26242=ORIENTED_EDGE('',*,*,#17507,.F.);
#26243=ORIENTED_EDGE('',*,*,#17379,.F.);
#26244=ORIENTED_EDGE('',*,*,#17376,.F.);
#26245=ORIENTED_EDGE('',*,*,#17373,.F.);
#26246=ORIENTED_EDGE('',*,*,#17369,.F.);
#26247=ORIENTED_EDGE('',*,*,#17381,.F.);
#26248=ORIENTED_EDGE('',*,*,#17306,.T.);
#26249=ORIENTED_EDGE('',*,*,#17509,.F.);
#26250=ORIENTED_EDGE('',*,*,#17510,.F.);
#26251=ORIENTED_EDGE('',*,*,#17511,.T.);
#26252=ORIENTED_EDGE('',*,*,#17310,.T.);
#26253=ORIENTED_EDGE('',*,*,#17406,.F.);
#26254=ORIENTED_EDGE('',*,*,#17366,.F.);
#26255=ORIENTED_EDGE('',*,*,#17512,.T.);
#26256=ORIENTED_EDGE('',*,*,#17513,.T.);
#26257=ORIENTED_EDGE('',*,*,#17311,.T.);
#26258=ORIENTED_EDGE('',*,*,#17511,.F.);
#26259=ORIENTED_EDGE('',*,*,#17514,.F.);
#26260=ORIENTED_EDGE('',*,*,#17515,.T.);
#26261=ORIENTED_EDGE('',*,*,#17312,.T.);
#26262=ORIENTED_EDGE('',*,*,#17513,.F.);
#26263=ORIENTED_EDGE('',*,*,#17516,.T.);
#26264=ORIENTED_EDGE('',*,*,#17517,.T.);
#26265=ORIENTED_EDGE('',*,*,#17313,.T.);
#26266=ORIENTED_EDGE('',*,*,#17515,.F.);
#26267=ORIENTED_EDGE('',*,*,#17518,.F.);
#26268=ORIENTED_EDGE('',*,*,#17519,.T.);
#26269=ORIENTED_EDGE('',*,*,#17314,.T.);
#26270=ORIENTED_EDGE('',*,*,#17517,.F.);
#26271=ORIENTED_EDGE('',*,*,#17520,.T.);
#26272=ORIENTED_EDGE('',*,*,#17521,.T.);
#26273=ORIENTED_EDGE('',*,*,#17315,.T.);
#26274=ORIENTED_EDGE('',*,*,#17519,.F.);
#26275=ORIENTED_EDGE('',*,*,#17522,.F.);
#26276=ORIENTED_EDGE('',*,*,#17523,.T.);
#26277=ORIENTED_EDGE('',*,*,#17316,.T.);
#26278=ORIENTED_EDGE('',*,*,#17521,.F.);
#26279=ORIENTED_EDGE('',*,*,#17524,.F.);
#26280=ORIENTED_EDGE('',*,*,#17525,.T.);
#26281=ORIENTED_EDGE('',*,*,#17317,.T.);
#26282=ORIENTED_EDGE('',*,*,#17523,.F.);
#26283=ORIENTED_EDGE('',*,*,#17263,.F.);
#26284=ORIENTED_EDGE('',*,*,#17260,.F.);
#26285=ORIENTED_EDGE('',*,*,#17318,.T.);
#26286=ORIENTED_EDGE('',*,*,#17525,.F.);
#26287=ORIENTED_EDGE('',*,*,#17526,.F.);
#26288=ORIENTED_EDGE('',*,*,#17527,.T.);
#26289=ORIENTED_EDGE('',*,*,#17264,.F.);
#26290=ORIENTED_EDGE('',*,*,#17527,.F.);
#26291=ORIENTED_EDGE('',*,*,#17528,.T.);
#26292=ORIENTED_EDGE('',*,*,#17281,.T.);
#26293=ORIENTED_EDGE('',*,*,#17528,.F.);
#26294=ORIENTED_EDGE('',*,*,#17526,.T.);
#26295=ORIENTED_EDGE('',*,*,#17524,.T.);
#26296=ORIENTED_EDGE('',*,*,#17522,.T.);
#26297=ORIENTED_EDGE('',*,*,#17520,.F.);
#26298=ORIENTED_EDGE('',*,*,#17518,.T.);
#26299=ORIENTED_EDGE('',*,*,#17516,.F.);
#26300=ORIENTED_EDGE('',*,*,#17514,.T.);
#26301=ORIENTED_EDGE('',*,*,#17512,.F.);
#26302=ORIENTED_EDGE('',*,*,#17510,.T.);
#26303=ORIENTED_EDGE('',*,*,#17508,.F.);
#26304=ORIENTED_EDGE('',*,*,#17506,.F.);
#26305=ORIENTED_EDGE('',*,*,#17504,.F.);
#26306=ORIENTED_EDGE('',*,*,#17478,.F.);
#26307=ORIENTED_EDGE('',*,*,#17503,.F.);
#26308=ORIENTED_EDGE('',*,*,#17501,.F.);
#26309=ORIENTED_EDGE('',*,*,#17499,.F.);
#26310=ORIENTED_EDGE('',*,*,#17497,.F.);
#26311=ORIENTED_EDGE('',*,*,#17495,.F.);
#26312=ORIENTED_EDGE('',*,*,#17493,.F.);
#26313=ORIENTED_EDGE('',*,*,#17491,.T.);
#26314=ORIENTED_EDGE('',*,*,#17285,.F.);
#26315=ORIENTED_EDGE('',*,*,#17490,.F.);
#26316=ORIENTED_EDGE('',*,*,#17488,.F.);
#26317=ORIENTED_EDGE('',*,*,#17288,.F.);
#26318=ORIENTED_EDGE('',*,*,#17282,.T.);
#26319=ORIENTED_EDGE('',*,*,#17338,.F.);
#26320=ORIENTED_EDGE('',*,*,#16177,.F.);
#26321=ORIENTED_EDGE('',*,*,#17337,.F.);
#26322=ORIENTED_EDGE('',*,*,#17096,.F.);
#26323=ORIENTED_EDGE('',*,*,#17340,.F.);
#26324=ORIENTED_EDGE('',*,*,#16313,.F.);
#26325=ORIENTED_EDGE('',*,*,#17339,.F.);
#26326=ORIENTED_EDGE('',*,*,#16980,.F.);
#26327=ORIENTED_EDGE('',*,*,#17342,.F.);
#26328=ORIENTED_EDGE('',*,*,#16449,.F.);
#26329=ORIENTED_EDGE('',*,*,#17341,.F.);
#26330=ORIENTED_EDGE('',*,*,#16864,.F.);
#26331=ORIENTED_EDGE('',*,*,#17344,.F.);
#26332=ORIENTED_EDGE('',*,*,#16585,.F.);
#26333=ORIENTED_EDGE('',*,*,#17343,.F.);
#26334=ORIENTED_EDGE('',*,*,#16748,.F.);
#26694=PLANE('',#29994);
#26695=PLANE('',#29998);
#26696=PLANE('',#30003);
#26697=PLANE('',#30007);
#26698=PLANE('',#30012);
#26699=PLANE('',#30013);
#26700=PLANE('',#30014);
#26701=PLANE('',#30015);
#26702=PLANE('',#30016);
#26703=PLANE('',#30029);
#26704=PLANE('',#30030);
#26705=PLANE('',#30031);
#26706=PLANE('',#30032);
#26707=PLANE('',#30033);
#26708=PLANE('',#30034);
#26709=PLANE('',#30035);
#26710=PLANE('',#30039);
#26711=PLANE('',#30043);
#26712=PLANE('',#30047);
#26713=PLANE('',#30048);
#26714=PLANE('',#30049);
#26715=PLANE('',#30052);
#26716=PLANE('',#30053);
#26717=PLANE('',#30054);
#26718=PLANE('',#30055);
#26719=PLANE('',#30056);
#26720=PLANE('',#30057);
#26721=PLANE('',#30058);
#26722=PLANE('',#30062);
#26723=PLANE('',#30063);
#26724=PLANE('',#30064);
#26725=PLANE('',#30067);
#26726=PLANE('',#30068);
#26727=PLANE('',#30071);
#26728=PLANE('',#30075);
#26729=PLANE('',#30079);
#26730=PLANE('',#30080);
#26731=PLANE('',#30081);
#26732=PLANE('',#30084);
#26733=PLANE('',#30085);
#26734=PLANE('',#30086);
#26735=PLANE('',#30087);
#26736=PLANE('',#30088);
#26737=PLANE('',#30089);
#26738=PLANE('',#30090);
#26739=PLANE('',#30094);
#26740=PLANE('',#30095);
#26741=PLANE('',#30096);
#26742=PLANE('',#30097);
#26743=PLANE('',#30098);
#26744=PLANE('',#30099);
#26745=PLANE('',#30100);
#26746=PLANE('',#30101);
#26747=PLANE('',#30105);
#26748=PLANE('',#30106);
#26749=PLANE('',#30107);
#26750=PLANE('',#30108);
#26751=PLANE('',#30109);
#26752=PLANE('',#30112);
#26753=PLANE('',#30115);
#26754=PLANE('',#30118);
#26755=PLANE('',#30121);
#26756=PLANE('',#30122);
#26757=PLANE('',#30127);
#26758=PLANE('',#30130);
#26759=PLANE('',#30133);
#26760=PLANE('',#30138);
#26761=PLANE('',#30141);
#26762=PLANE('',#30144);
#26763=PLANE('',#30147);
#26764=PLANE('',#30150);
#26765=PLANE('',#30153);
#26766=PLANE('',#30156);
#27720=ADVANCED_FACE('',(#3917),#2689,.F.);
#27721=ADVANCED_FACE('',(#3918),#2690,.F.);
#27722=ADVANCED_FACE('',(#3919),#2691,.F.);
#27723=ADVANCED_FACE('',(#3920),#2692,.F.);
#27724=ADVANCED_FACE('',(#3921),#2693,.F.);
#27725=ADVANCED_FACE('',(#3922),#2694,.F.);
#27726=ADVANCED_FACE('',(#3923),#2695,.F.);
#27727=ADVANCED_FACE('',(#3924),#2696,.F.);
#27728=ADVANCED_FACE('',(#3925),#2697,.F.);
#27729=ADVANCED_FACE('',(#3926),#2698,.F.);
#27730=ADVANCED_FACE('',(#3927),#2699,.F.);
#27731=ADVANCED_FACE('',(#3928),#2700,.F.);
#27732=ADVANCED_FACE('',(#3929),#2701,.F.);
#27733=ADVANCED_FACE('',(#3930),#2702,.F.);
#27734=ADVANCED_FACE('',(#3931),#2703,.F.);
#27735=ADVANCED_FACE('',(#3932),#2704,.F.);
#27736=ADVANCED_FACE('',(#3933),#2705,.F.);
#27737=ADVANCED_FACE('',(#3934),#2706,.F.);
#27738=ADVANCED_FACE('',(#3935),#2707,.F.);
#27739=ADVANCED_FACE('',(#3936),#2708,.F.);
#27740=ADVANCED_FACE('',(#3937),#2709,.F.);
#27741=ADVANCED_FACE('',(#3938),#2710,.F.);
#27742=ADVANCED_FACE('',(#3939),#2711,.F.);
#27743=ADVANCED_FACE('',(#3940),#2712,.F.);
#27744=ADVANCED_FACE('',(#3941),#2713,.F.);
#27745=ADVANCED_FACE('',(#3942),#2714,.F.);
#27746=ADVANCED_FACE('',(#3943),#2715,.F.);
#27747=ADVANCED_FACE('',(#3944),#2716,.F.);
#27748=ADVANCED_FACE('',(#3945),#2717,.F.);
#27749=ADVANCED_FACE('',(#3946),#2718,.F.);
#27750=ADVANCED_FACE('',(#3947),#2719,.F.);
#27751=ADVANCED_FACE('',(#3948),#2720,.F.);
#27752=ADVANCED_FACE('',(#3949),#2721,.F.);
#27753=ADVANCED_FACE('',(#3950),#2722,.F.);
#27754=ADVANCED_FACE('',(#3951),#2723,.F.);
#27755=ADVANCED_FACE('',(#3952),#2724,.F.);
#27756=ADVANCED_FACE('',(#3953),#2725,.F.);
#27757=ADVANCED_FACE('',(#3954),#2726,.F.);
#27758=ADVANCED_FACE('',(#3955),#2727,.F.);
#27759=ADVANCED_FACE('',(#3956),#2728,.F.);
#27760=ADVANCED_FACE('',(#3957),#2729,.F.);
#27761=ADVANCED_FACE('',(#3958),#2730,.F.);
#27762=ADVANCED_FACE('',(#3959),#2731,.F.);
#27763=ADVANCED_FACE('',(#3960),#2732,.F.);
#27764=ADVANCED_FACE('',(#3961),#2733,.F.);
#27765=ADVANCED_FACE('',(#3962),#2734,.F.);
#27766=ADVANCED_FACE('',(#3963),#2735,.F.);
#27767=ADVANCED_FACE('',(#3964),#2736,.F.);
#27768=ADVANCED_FACE('',(#3965),#2737,.F.);
#27769=ADVANCED_FACE('',(#3966),#2738,.F.);
#27770=ADVANCED_FACE('',(#3967),#2739,.F.);
#27771=ADVANCED_FACE('',(#3968),#2740,.F.);
#27772=ADVANCED_FACE('',(#3969),#2741,.F.);
#27773=ADVANCED_FACE('',(#3970),#2742,.F.);
#27774=ADVANCED_FACE('',(#3971),#2743,.F.);
#27775=ADVANCED_FACE('',(#3972),#2744,.F.);
#27776=ADVANCED_FACE('',(#3973),#2745,.F.);
#27777=ADVANCED_FACE('',(#3974),#2746,.F.);
#27778=ADVANCED_FACE('',(#3975),#2747,.F.);
#27779=ADVANCED_FACE('',(#3976),#2748,.F.);
#27780=ADVANCED_FACE('',(#3977),#2749,.F.);
#27781=ADVANCED_FACE('',(#3978),#2750,.F.);
#27782=ADVANCED_FACE('',(#3979),#2751,.F.);
#27783=ADVANCED_FACE('',(#3980),#2752,.F.);
#27784=ADVANCED_FACE('',(#3981),#2753,.F.);
#27785=ADVANCED_FACE('',(#3982),#2754,.F.);
#27786=ADVANCED_FACE('',(#3983),#2755,.F.);
#27787=ADVANCED_FACE('',(#3984),#2756,.F.);
#27788=ADVANCED_FACE('',(#3985),#2757,.F.);
#27789=ADVANCED_FACE('',(#3986),#2758,.F.);
#27790=ADVANCED_FACE('',(#3987),#2759,.F.);
#27791=ADVANCED_FACE('',(#3988),#2760,.F.);
#27792=ADVANCED_FACE('',(#3989),#2761,.F.);
#27793=ADVANCED_FACE('',(#3990),#2762,.F.);
#27794=ADVANCED_FACE('',(#3991),#2763,.F.);
#27795=ADVANCED_FACE('',(#3992),#2764,.F.);
#27796=ADVANCED_FACE('',(#3993),#2765,.F.);
#27797=ADVANCED_FACE('',(#3994),#2766,.F.);
#27798=ADVANCED_FACE('',(#3995),#2767,.F.);
#27799=ADVANCED_FACE('',(#3996),#2768,.F.);
#27800=ADVANCED_FACE('',(#3997),#2769,.F.);
#27801=ADVANCED_FACE('',(#3998),#2770,.F.);
#27802=ADVANCED_FACE('',(#3999),#2771,.F.);
#27803=ADVANCED_FACE('',(#4000),#2772,.F.);
#27804=ADVANCED_FACE('',(#4001),#2773,.F.);
#27805=ADVANCED_FACE('',(#4002),#2774,.F.);
#27806=ADVANCED_FACE('',(#4003),#2775,.F.);
#27807=ADVANCED_FACE('',(#4004),#2776,.F.);
#27808=ADVANCED_FACE('',(#4005),#2777,.F.);
#27809=ADVANCED_FACE('',(#4006),#2778,.F.);
#27810=ADVANCED_FACE('',(#4007),#2779,.F.);
#27811=ADVANCED_FACE('',(#4008),#2780,.F.);
#27812=ADVANCED_FACE('',(#4009),#2781,.F.);
#27813=ADVANCED_FACE('',(#4010),#2782,.F.);
#27814=ADVANCED_FACE('',(#4011),#2783,.F.);
#27815=ADVANCED_FACE('',(#4012),#2784,.F.);
#27816=ADVANCED_FACE('',(#4013),#2785,.F.);
#27817=ADVANCED_FACE('',(#4014),#2786,.F.);
#27818=ADVANCED_FACE('',(#4015),#2787,.F.);
#27819=ADVANCED_FACE('',(#4016),#2788,.F.);
#27820=ADVANCED_FACE('',(#4017),#2789,.F.);
#27821=ADVANCED_FACE('',(#4018),#2790,.F.);
#27822=ADVANCED_FACE('',(#4019),#2791,.F.);
#27823=ADVANCED_FACE('',(#4020),#2792,.F.);
#27824=ADVANCED_FACE('',(#4021),#2793,.F.);
#27825=ADVANCED_FACE('',(#4022),#2794,.F.);
#27826=ADVANCED_FACE('',(#4023),#2795,.F.);
#27827=ADVANCED_FACE('',(#4024),#2796,.F.);
#27828=ADVANCED_FACE('',(#4025),#2797,.F.);
#27829=ADVANCED_FACE('',(#4026),#2798,.F.);
#27830=ADVANCED_FACE('',(#4027),#2799,.F.);
#27831=ADVANCED_FACE('',(#4028),#2800,.F.);
#27832=ADVANCED_FACE('',(#4029),#2801,.F.);
#27833=ADVANCED_FACE('',(#4030),#2802,.F.);
#27834=ADVANCED_FACE('',(#4031),#2803,.F.);
#27835=ADVANCED_FACE('',(#4032),#2804,.F.);
#27836=ADVANCED_FACE('',(#4033),#2805,.F.);
#27837=ADVANCED_FACE('',(#4034),#2806,.F.);
#27838=ADVANCED_FACE('',(#4035),#2807,.F.);
#27839=ADVANCED_FACE('',(#4036),#2808,.F.);
#27840=ADVANCED_FACE('',(#4037),#2809,.F.);
#27841=ADVANCED_FACE('',(#4038),#2810,.F.);
#27842=ADVANCED_FACE('',(#4039),#2811,.F.);
#27843=ADVANCED_FACE('',(#4040),#2812,.F.);
#27844=ADVANCED_FACE('',(#4041),#2813,.F.);
#27845=ADVANCED_FACE('',(#4042),#2814,.F.);
#27846=ADVANCED_FACE('',(#4043),#2815,.F.);
#27847=ADVANCED_FACE('',(#4044),#2816,.F.);
#27848=ADVANCED_FACE('',(#4045),#2817,.F.);
#27849=ADVANCED_FACE('',(#4046),#2818,.F.);
#27850=ADVANCED_FACE('',(#4047),#2819,.F.);
#27851=ADVANCED_FACE('',(#4048),#2820,.F.);
#27852=ADVANCED_FACE('',(#4049),#2821,.F.);
#27853=ADVANCED_FACE('',(#4050),#2822,.F.);
#27854=ADVANCED_FACE('',(#4051),#2823,.F.);
#27855=ADVANCED_FACE('',(#4052),#2824,.F.);
#27856=ADVANCED_FACE('',(#4053),#2825,.F.);
#27857=ADVANCED_FACE('',(#4054),#2826,.F.);
#27858=ADVANCED_FACE('',(#4055),#2827,.F.);
#27859=ADVANCED_FACE('',(#4056),#2828,.F.);
#27860=ADVANCED_FACE('',(#4057),#2829,.F.);
#27861=ADVANCED_FACE('',(#4058),#2830,.F.);
#27862=ADVANCED_FACE('',(#4059),#2831,.F.);
#27863=ADVANCED_FACE('',(#4060),#2832,.F.);
#27864=ADVANCED_FACE('',(#4061),#2833,.F.);
#27865=ADVANCED_FACE('',(#4062),#2834,.F.);
#27866=ADVANCED_FACE('',(#4063),#2835,.F.);
#27867=ADVANCED_FACE('',(#4064),#2836,.F.);
#27868=ADVANCED_FACE('',(#4065),#2837,.F.);
#27869=ADVANCED_FACE('',(#4066),#2838,.F.);
#27870=ADVANCED_FACE('',(#4067),#2839,.F.);
#27871=ADVANCED_FACE('',(#4068),#2840,.F.);
#27872=ADVANCED_FACE('',(#4069),#2841,.F.);
#27873=ADVANCED_FACE('',(#4070),#2842,.F.);
#27874=ADVANCED_FACE('',(#4071),#2843,.F.);
#27875=ADVANCED_FACE('',(#4072),#2844,.F.);
#27876=ADVANCED_FACE('',(#4073),#2845,.F.);
#27877=ADVANCED_FACE('',(#4074),#2846,.F.);
#27878=ADVANCED_FACE('',(#4075),#2847,.F.);
#27879=ADVANCED_FACE('',(#4076),#2848,.F.);
#27880=ADVANCED_FACE('',(#4077),#2849,.F.);
#27881=ADVANCED_FACE('',(#4078),#2850,.F.);
#27882=ADVANCED_FACE('',(#4079),#2851,.F.);
#27883=ADVANCED_FACE('',(#4080),#2852,.F.);
#27884=ADVANCED_FACE('',(#4081),#2853,.F.);
#27885=ADVANCED_FACE('',(#4082),#2854,.F.);
#27886=ADVANCED_FACE('',(#4083),#2855,.F.);
#27887=ADVANCED_FACE('',(#4084),#2856,.F.);
#27888=ADVANCED_FACE('',(#4085),#2857,.F.);
#27889=ADVANCED_FACE('',(#4086),#2858,.F.);
#27890=ADVANCED_FACE('',(#4087),#2859,.F.);
#27891=ADVANCED_FACE('',(#4088),#2860,.F.);
#27892=ADVANCED_FACE('',(#4089),#2861,.F.);
#27893=ADVANCED_FACE('',(#4090),#2862,.F.);
#27894=ADVANCED_FACE('',(#4091),#2863,.F.);
#27895=ADVANCED_FACE('',(#4092),#2864,.F.);
#27896=ADVANCED_FACE('',(#4093),#2865,.F.);
#27897=ADVANCED_FACE('',(#4094),#2866,.F.);
#27898=ADVANCED_FACE('',(#4095),#2867,.F.);
#27899=ADVANCED_FACE('',(#4096),#2868,.F.);
#27900=ADVANCED_FACE('',(#4097),#2869,.F.);
#27901=ADVANCED_FACE('',(#4098),#2870,.F.);
#27902=ADVANCED_FACE('',(#4099),#2871,.F.);
#27903=ADVANCED_FACE('',(#4100),#2872,.F.);
#27904=ADVANCED_FACE('',(#4101),#2873,.F.);
#27905=ADVANCED_FACE('',(#4102),#2874,.F.);
#27906=ADVANCED_FACE('',(#4103),#2875,.F.);
#27907=ADVANCED_FACE('',(#4104),#2876,.F.);
#27908=ADVANCED_FACE('',(#4105),#2877,.F.);
#27909=ADVANCED_FACE('',(#4106),#2878,.F.);
#27910=ADVANCED_FACE('',(#4107),#2879,.F.);
#27911=ADVANCED_FACE('',(#4108),#2880,.F.);
#27912=ADVANCED_FACE('',(#4109),#2881,.F.);
#27913=ADVANCED_FACE('',(#4110),#2882,.F.);
#27914=ADVANCED_FACE('',(#4111),#2883,.F.);
#27915=ADVANCED_FACE('',(#4112),#2884,.F.);
#27916=ADVANCED_FACE('',(#4113),#2885,.F.);
#27917=ADVANCED_FACE('',(#4114),#2886,.F.);
#27918=ADVANCED_FACE('',(#4115),#2887,.F.);
#27919=ADVANCED_FACE('',(#4116),#2888,.F.);
#27920=ADVANCED_FACE('',(#4117),#2889,.F.);
#27921=ADVANCED_FACE('',(#4118),#2890,.F.);
#27922=ADVANCED_FACE('',(#4119),#2891,.F.);
#27923=ADVANCED_FACE('',(#4120),#2892,.F.);
#27924=ADVANCED_FACE('',(#4121),#2893,.F.);
#27925=ADVANCED_FACE('',(#4122),#2894,.F.);
#27926=ADVANCED_FACE('',(#4123),#2895,.F.);
#27927=ADVANCED_FACE('',(#4124),#2896,.F.);
#27928=ADVANCED_FACE('',(#4125),#2897,.F.);
#27929=ADVANCED_FACE('',(#4126),#2898,.F.);
#27930=ADVANCED_FACE('',(#4127),#2899,.F.);
#27931=ADVANCED_FACE('',(#4128),#2900,.F.);
#27932=ADVANCED_FACE('',(#4129),#2901,.F.);
#27933=ADVANCED_FACE('',(#4130),#2902,.F.);
#27934=ADVANCED_FACE('',(#4131),#2903,.F.);
#27935=ADVANCED_FACE('',(#4132),#2904,.F.);
#27936=ADVANCED_FACE('',(#4133),#2905,.F.);
#27937=ADVANCED_FACE('',(#4134),#2906,.F.);
#27938=ADVANCED_FACE('',(#4135),#2907,.F.);
#27939=ADVANCED_FACE('',(#4136),#2908,.F.);
#27940=ADVANCED_FACE('',(#4137),#2909,.F.);
#27941=ADVANCED_FACE('',(#4138),#2910,.F.);
#27942=ADVANCED_FACE('',(#4139),#2911,.F.);
#27943=ADVANCED_FACE('',(#4140),#2912,.F.);
#27944=ADVANCED_FACE('',(#4141),#2913,.F.);
#27945=ADVANCED_FACE('',(#4142),#2914,.F.);
#27946=ADVANCED_FACE('',(#4143),#2915,.F.);
#27947=ADVANCED_FACE('',(#4144),#2916,.F.);
#27948=ADVANCED_FACE('',(#4145),#2917,.F.);
#27949=ADVANCED_FACE('',(#4146),#2918,.F.);
#27950=ADVANCED_FACE('',(#4147),#2919,.F.);
#27951=ADVANCED_FACE('',(#4148),#2920,.F.);
#27952=ADVANCED_FACE('',(#4149),#2921,.F.);
#27953=ADVANCED_FACE('',(#4150),#2922,.F.);
#27954=ADVANCED_FACE('',(#4151),#2923,.F.);
#27955=ADVANCED_FACE('',(#4152),#2924,.F.);
#27956=ADVANCED_FACE('',(#4153),#2925,.F.);
#27957=ADVANCED_FACE('',(#4154),#2926,.F.);
#27958=ADVANCED_FACE('',(#4155),#2927,.F.);
#27959=ADVANCED_FACE('',(#4156),#2928,.F.);
#27960=ADVANCED_FACE('',(#4157),#2929,.F.);
#27961=ADVANCED_FACE('',(#4158),#2930,.F.);
#27962=ADVANCED_FACE('',(#4159),#2931,.F.);
#27963=ADVANCED_FACE('',(#4160),#2932,.F.);
#27964=ADVANCED_FACE('',(#4161),#2933,.F.);
#27965=ADVANCED_FACE('',(#4162),#26694,.F.);
#27966=ADVANCED_FACE('',(#4163),#2934,.F.);
#27967=ADVANCED_FACE('',(#4164),#26695,.F.);
#27968=ADVANCED_FACE('',(#4165),#2935,.F.);
#27969=ADVANCED_FACE('',(#4166),#26696,.F.);
#27970=ADVANCED_FACE('',(#4167),#2936,.F.);
#27971=ADVANCED_FACE('',(#4168),#26697,.F.);
#27972=ADVANCED_FACE('',(#4169),#2937,.F.);
#27973=ADVANCED_FACE('',(#4170),#26698,.F.);
#27974=ADVANCED_FACE('',(#4171),#26699,.F.);
#27975=ADVANCED_FACE('',(#4172),#26700,.F.);
#27976=ADVANCED_FACE('',(#4173),#26701,.F.);
#27977=ADVANCED_FACE('',(#4174,#220,#221,#222,#223,#224,#225,#226,#227,
#228),#26702,.T.);
#27978=ADVANCED_FACE('',(#4175),#161,.T.);
#27979=ADVANCED_FACE('',(#4176),#162,.T.);
#27980=ADVANCED_FACE('',(#4177),#163,.T.);
#27981=ADVANCED_FACE('',(#4178),#164,.T.);
#27982=ADVANCED_FACE('',(#4179),#165,.T.);
#27983=ADVANCED_FACE('',(#4180),#166,.T.);
#27984=ADVANCED_FACE('',(#4181),#167,.T.);
#27985=ADVANCED_FACE('',(#4182),#168,.T.);
#27986=ADVANCED_FACE('',(#4183),#169,.T.);
#27987=ADVANCED_FACE('',(#4184),#170,.T.);
#27988=ADVANCED_FACE('',(#4185),#171,.T.);
#27989=ADVANCED_FACE('',(#4186),#172,.T.);
#27990=ADVANCED_FACE('',(#4187),#26703,.F.);
#27991=ADVANCED_FACE('',(#4188),#26704,.F.);
#27992=ADVANCED_FACE('',(#4189),#26705,.F.);
#27993=ADVANCED_FACE('',(#4190),#26706,.F.);
#27994=ADVANCED_FACE('',(#4191),#26707,.F.);
#27995=ADVANCED_FACE('',(#4192),#26708,.F.);
#27996=ADVANCED_FACE('',(#4193),#26709,.F.);
#27997=ADVANCED_FACE('',(#4194),#2938,.F.);
#27998=ADVANCED_FACE('',(#4195,#229),#26710,.T.);
#27999=ADVANCED_FACE('',(#4196),#2939,.F.);
#28000=ADVANCED_FACE('',(#4197),#26711,.F.);
#28001=ADVANCED_FACE('',(#4198),#2940,.F.);
#28002=ADVANCED_FACE('',(#4199),#26712,.F.);
#28003=ADVANCED_FACE('',(#4200),#26713,.F.);
#28004=ADVANCED_FACE('',(#4201,#230,#231,#232),#26714,.T.);
#28005=ADVANCED_FACE('',(#4202),#26715,.F.);
#28006=ADVANCED_FACE('',(#4203),#26716,.F.);
#28007=ADVANCED_FACE('',(#4204),#26717,.F.);
#28008=ADVANCED_FACE('',(#4205),#26718,.F.);
#28009=ADVANCED_FACE('',(#4206),#26719,.F.);
#28010=ADVANCED_FACE('',(#4207),#26720,.F.);
#28011=ADVANCED_FACE('',(#4208),#26721,.F.);
#28012=ADVANCED_FACE('',(#4209),#2941,.F.);
#28013=ADVANCED_FACE('',(#4210,#233),#26722,.T.);
#28014=ADVANCED_FACE('',(#4211),#26723,.F.);
#28015=ADVANCED_FACE('',(#4212),#26724,.F.);
#28016=ADVANCED_FACE('',(#4213),#2942,.F.);
#28017=ADVANCED_FACE('',(#4214),#26725,.T.);
#28018=ADVANCED_FACE('',(#4215),#26726,.T.);
#28019=ADVANCED_FACE('',(#4216),#2943,.F.);
#28020=ADVANCED_FACE('',(#4217),#26727,.T.);
#28021=ADVANCED_FACE('',(#4218),#2944,.F.);
#28022=ADVANCED_FACE('',(#4219),#26728,.T.);
#28023=ADVANCED_FACE('',(#4220),#2945,.F.);
#28024=ADVANCED_FACE('',(#4221),#26729,.T.);
#28025=ADVANCED_FACE('',(#4222),#26730,.T.);
#28026=ADVANCED_FACE('',(#4223,#234,#235,#236),#26731,.F.);
#28027=ADVANCED_FACE('',(#4224),#26732,.T.);
#28028=ADVANCED_FACE('',(#4225),#26733,.T.);
#28029=ADVANCED_FACE('',(#4226),#26734,.T.);
#28030=ADVANCED_FACE('',(#4227),#26735,.T.);
#28031=ADVANCED_FACE('',(#4228),#26736,.T.);
#28032=ADVANCED_FACE('',(#4229),#26737,.T.);
#28033=ADVANCED_FACE('',(#4230),#26738,.T.);
#28034=ADVANCED_FACE('',(#4231),#2946,.F.);
#28035=ADVANCED_FACE('',(#4232,#237),#26739,.F.);
#28036=ADVANCED_FACE('',(#4233),#26740,.T.);
#28037=ADVANCED_FACE('',(#4234),#26741,.T.);
#28038=ADVANCED_FACE('',(#4235),#26742,.T.);
#28039=ADVANCED_FACE('',(#4236),#26743,.T.);
#28040=ADVANCED_FACE('',(#4237),#26744,.T.);
#28041=ADVANCED_FACE('',(#4238),#26745,.T.);
#28042=ADVANCED_FACE('',(#4239),#26746,.T.);
#28043=ADVANCED_FACE('',(#4240),#2947,.F.);
#28044=ADVANCED_FACE('',(#4241,#238),#26747,.F.);
#28045=ADVANCED_FACE('',(#4242),#26748,.F.);
#28046=ADVANCED_FACE('',(#4243),#26749,.F.);
#28047=ADVANCED_FACE('',(#4244,#239,#240),#26750,.F.);
#28048=ADVANCED_FACE('',(#4245),#26751,.F.);
#28049=ADVANCED_FACE('',(#4246),#2948,.F.);
#28050=ADVANCED_FACE('',(#4247),#26752,.F.);
#28051=ADVANCED_FACE('',(#4248),#2949,.F.);
#28052=ADVANCED_FACE('',(#4249),#26753,.F.);
#28053=ADVANCED_FACE('',(#4250),#2950,.F.);
#28054=ADVANCED_FACE('',(#4251),#26754,.F.);
#28055=ADVANCED_FACE('',(#4252),#2951,.F.);
#28056=ADVANCED_FACE('',(#4253),#26755,.F.);
#28057=ADVANCED_FACE('',(#4254),#26756,.F.);
#28058=ADVANCED_FACE('',(#4255),#2952,.T.);
#28059=ADVANCED_FACE('',(#4256),#2953,.F.);
#28060=ADVANCED_FACE('',(#4257),#26757,.F.);
#28061=ADVANCED_FACE('',(#4258),#2954,.T.);
#28062=ADVANCED_FACE('',(#4259),#26758,.F.);
#28063=ADVANCED_FACE('',(#4260),#2955,.T.);
#28064=ADVANCED_FACE('',(#4261),#26759,.F.);
#28065=ADVANCED_FACE('',(#4262),#2956,.T.);
#28066=ADVANCED_FACE('',(#4263),#2957,.T.);
#28067=ADVANCED_FACE('',(#4264),#26760,.F.);
#28068=ADVANCED_FACE('',(#4265),#2958,.T.);
#28069=ADVANCED_FACE('',(#4266,#241,#242),#26761,.F.);
#28070=ADVANCED_FACE('',(#4267),#2959,.T.);
#28071=ADVANCED_FACE('',(#4268),#26762,.F.);
#28072=ADVANCED_FACE('',(#4269),#2960,.T.);
#28073=ADVANCED_FACE('',(#4270),#26763,.F.);
#28074=ADVANCED_FACE('',(#4271),#2961,.T.);
#28075=ADVANCED_FACE('',(#4272),#26764,.F.);
#28076=ADVANCED_FACE('',(#4273),#2962,.F.);
#28077=ADVANCED_FACE('',(#4274),#26765,.F.);
#28078=ADVANCED_FACE('',(#4275),#2963,.T.);
#28079=ADVANCED_FACE('',(#4276,#243,#244,#245,#246),#26766,.F.);
#28088=CLOSED_SHELL('',(#27720,#27721,#27722,#27723,#27724,#27725,#27726,
#27727,#27728,#27729,#27730,#27731,#27732,#27733,#27734,#27735,#27736,#27737,
#27738,#27739,#27740,#27741,#27742,#27743,#27744,#27745,#27746,#27747,#27748,
#27749,#27750,#27751,#27752,#27753,#27754,#27755,#27756,#27757,#27758,#27759,
#27760,#27761,#27762,#27763,#27764,#27765,#27766,#27767,#27768,#27769,#27770,
#27771,#27772,#27773,#27774,#27775,#27776,#27777,#27778,#27779,#27780,#27781,
#27782,#27783,#27784,#27785,#27786,#27787,#27788,#27789,#27790,#27791,#27792,
#27793,#27794,#27795,#27796,#27797,#27798,#27799,#27800,#27801,#27802,#27803,
#27804,#27805,#27806,#27807,#27808,#27809,#27810,#27811,#27812,#27813,#27814,
#27815,#27816,#27817,#27818,#27819,#27820,#27821,#27822,#27823,#27824,#27825,
#27826,#27827,#27828,#27829,#27830,#27831,#27832,#27833,#27834,#27835,#27836,
#27837,#27838,#27839,#27840,#27841,#27842,#27843,#27844,#27845,#27846,#27847,
#27848,#27849,#27850,#27851,#27852,#27853,#27854,#27855,#27856,#27857,#27858,
#27859,#27860,#27861,#27862,#27863,#27864,#27865,#27866,#27867,#27868,#27869,
#27870,#27871,#27872,#27873,#27874,#27875,#27876,#27877,#27878,#27879,#27880,
#27881,#27882,#27883,#27884,#27885,#27886,#27887,#27888,#27889,#27890,#27891,
#27892,#27893,#27894,#27895,#27896,#27897,#27898,#27899,#27900,#27901,#27902,
#27903,#27904,#27905,#27906,#27907,#27908,#27909,#27910,#27911,#27912,#27913,
#27914,#27915,#27916,#27917,#27918,#27919,#27920,#27921,#27922,#27923,#27924,
#27925,#27926,#27927,#27928,#27929,#27930,#27931,#27932,#27933,#27934,#27935,
#27936,#27937,#27938,#27939,#27940,#27941,#27942,#27943,#27944,#27945,#27946,
#27947,#27948,#27949,#27950,#27951,#27952,#27953,#27954,#27955,#27956,#27957,
#27958,#27959,#27960,#27961,#27962,#27963,#27964,#27965,#27966,#27967,#27968,
#27969,#27970,#27971,#27972,#27973,#27974,#27975,#27976,#27977,#27978,#27979,
#27980,#27981,#27982,#27983,#27984,#27985,#27986,#27987,#27988,#27989,#27990,
#27991,#27992,#27993,#27994,#27995,#27996,#27997,#27998,#27999,#28000,#28001,
#28002,#28003,#28004,#28005,#28006,#28007,#28008,#28009,#28010,#28011,#28012,
#28013,#28014,#28015,#28016,#28017,#28018,#28019,#28020,#28021,#28022,#28023,
#28024,#28025,#28026,#28027,#28028,#28029,#28030,#28031,#28032,#28033,#28034,
#28035,#28036,#28037,#28038,#28039,#28040,#28041,#28042,#28043,#28044,#28045,
#28046,#28047,#28048,#28049,#28050,#28051,#28052,#28053,#28054,#28055,#28056,
#28057,#28058,#28059,#28060,#28061,#28062,#28063,#28064,#28065,#28066,#28067,
#28068,#28069,#28070,#28071,#28072,#28073,#28074,#28075,#28076,#28077,#28078,
#28079));
#29720=AXIS2_PLACEMENT_3D('',#128402,#34674,#34675);
#29721=AXIS2_PLACEMENT_3D('',#128403,#34676,#34677);
#29722=AXIS2_PLACEMENT_3D('',#128437,#34679,#34680);
#29723=AXIS2_PLACEMENT_3D('',#128442,#34681,#34682);
#29724=AXIS2_PLACEMENT_3D('',#128702,#34684,#34685);
#29725=AXIS2_PLACEMENT_3D('',#129146,#34687,#34688);
#29726=AXIS2_PLACEMENT_3D('',#129442,#34690,#34691);
#29727=AXIS2_PLACEMENT_3D('',#129476,#34693,#34694);
#29728=AXIS2_PLACEMENT_3D('',#129481,#34695,#34696);
#29729=AXIS2_PLACEMENT_3D('',#129741,#34698,#34699);
#29730=AXIS2_PLACEMENT_3D('',#130185,#34701,#34702);
#29731=AXIS2_PLACEMENT_3D('',#130481,#34704,#34705);
#29732=AXIS2_PLACEMENT_3D('',#130554,#34707,#34708);
#29733=AXIS2_PLACEMENT_3D('',#130569,#34709,#34710);
#29734=AXIS2_PLACEMENT_3D('',#130720,#34712,#34713);
#29735=AXIS2_PLACEMENT_3D('',#131053,#34715,#34716);
#29736=AXIS2_PLACEMENT_3D('',#131334,#34718,#34719);
#29737=AXIS2_PLACEMENT_3D('',#131670,#34721,#34722);
#29738=AXIS2_PLACEMENT_3D('',#131832,#34724,#34725);
#29739=AXIS2_PLACEMENT_3D('',#132102,#34727,#34728);
#29740=AXIS2_PLACEMENT_3D('',#132377,#34730,#34731);
#29741=AXIS2_PLACEMENT_3D('',#132711,#34733,#34734);
#29742=AXIS2_PLACEMENT_3D('',#132873,#34736,#34737);
#29743=AXIS2_PLACEMENT_3D('',#133140,#34739,#34740);
#29744=AXIS2_PLACEMENT_3D('',#133418,#34742,#34743);
#29745=AXIS2_PLACEMENT_3D('',#133751,#34745,#34746);
#29746=AXIS2_PLACEMENT_3D('',#133916,#34748,#34749);
#29747=AXIS2_PLACEMENT_3D('',#134185,#34751,#34752);
#29748=AXIS2_PLACEMENT_3D('',#134466,#34754,#34755);
#29749=AXIS2_PLACEMENT_3D('',#134799,#34757,#34758);
#29750=AXIS2_PLACEMENT_3D('',#134958,#34760,#34761);
#29751=AXIS2_PLACEMENT_3D('',#135228,#34763,#34764);
#29752=AXIS2_PLACEMENT_3D('',#135509,#34766,#34767);
#29753=AXIS2_PLACEMENT_3D('',#135840,#34769,#34770);
#29754=AXIS2_PLACEMENT_3D('',#136003,#34772,#34773);
#29755=AXIS2_PLACEMENT_3D('',#136269,#34775,#34776);
#29756=AXIS2_PLACEMENT_3D('',#136550,#34778,#34779);
#29757=AXIS2_PLACEMENT_3D('',#136883,#34781,#34782);
#29758=AXIS2_PLACEMENT_3D('',#137164,#34784,#34785);
#29759=AXIS2_PLACEMENT_3D('',#137262,#34787,#34788);
#29760=AXIS2_PLACEMENT_3D('',#137335,#34790,#34791);
#29761=AXIS2_PLACEMENT_3D('',#137350,#34792,#34793);
#29762=AXIS2_PLACEMENT_3D('',#137501,#34795,#34796);
#29763=AXIS2_PLACEMENT_3D('',#137834,#34798,#34799);
#29764=AXIS2_PLACEMENT_3D('',#138115,#34801,#34802);
#29765=AXIS2_PLACEMENT_3D('',#138451,#34804,#34805);
#29766=AXIS2_PLACEMENT_3D('',#138613,#34807,#34808);
#29767=AXIS2_PLACEMENT_3D('',#138883,#34810,#34811);
#29768=AXIS2_PLACEMENT_3D('',#139158,#34813,#34814);
#29769=AXIS2_PLACEMENT_3D('',#139492,#34816,#34817);
#29770=AXIS2_PLACEMENT_3D('',#139654,#34819,#34820);
#29771=AXIS2_PLACEMENT_3D('',#139921,#34822,#34823);
#29772=AXIS2_PLACEMENT_3D('',#140199,#34825,#34826);
#29773=AXIS2_PLACEMENT_3D('',#140532,#34828,#34829);
#29774=AXIS2_PLACEMENT_3D('',#140697,#34831,#34832);
#29775=AXIS2_PLACEMENT_3D('',#140966,#34834,#34835);
#29776=AXIS2_PLACEMENT_3D('',#141247,#34837,#34838);
#29777=AXIS2_PLACEMENT_3D('',#141580,#34840,#34841);
#29778=AXIS2_PLACEMENT_3D('',#141739,#34843,#34844);
#29779=AXIS2_PLACEMENT_3D('',#142009,#34846,#34847);
#29780=AXIS2_PLACEMENT_3D('',#142290,#34849,#34850);
#29781=AXIS2_PLACEMENT_3D('',#142621,#34852,#34853);
#29782=AXIS2_PLACEMENT_3D('',#142784,#34855,#34856);
#29783=AXIS2_PLACEMENT_3D('',#143050,#34858,#34859);
#29784=AXIS2_PLACEMENT_3D('',#143331,#34861,#34862);
#29785=AXIS2_PLACEMENT_3D('',#143664,#34864,#34865);
#29786=AXIS2_PLACEMENT_3D('',#143945,#34867,#34868);
#29787=AXIS2_PLACEMENT_3D('',#144043,#34870,#34871);
#29788=AXIS2_PLACEMENT_3D('',#144116,#34873,#34874);
#29789=AXIS2_PLACEMENT_3D('',#144131,#34875,#34876);
#29790=AXIS2_PLACEMENT_3D('',#144282,#34878,#34879);
#29791=AXIS2_PLACEMENT_3D('',#144615,#34881,#34882);
#29792=AXIS2_PLACEMENT_3D('',#144896,#34884,#34885);
#29793=AXIS2_PLACEMENT_3D('',#145232,#34887,#34888);
#29794=AXIS2_PLACEMENT_3D('',#145394,#34890,#34891);
#29795=AXIS2_PLACEMENT_3D('',#145664,#34893,#34894);
#29796=AXIS2_PLACEMENT_3D('',#145939,#34896,#34897);
#29797=AXIS2_PLACEMENT_3D('',#146273,#34899,#34900);
#29798=AXIS2_PLACEMENT_3D('',#146435,#34902,#34903);
#29799=AXIS2_PLACEMENT_3D('',#146702,#34905,#34906);
#29800=AXIS2_PLACEMENT_3D('',#146980,#34908,#34909);
#29801=AXIS2_PLACEMENT_3D('',#147313,#34911,#34912);
#29802=AXIS2_PLACEMENT_3D('',#147478,#34914,#34915);
#29803=AXIS2_PLACEMENT_3D('',#147747,#34917,#34918);
#29804=AXIS2_PLACEMENT_3D('',#148028,#34920,#34921);
#29805=AXIS2_PLACEMENT_3D('',#148361,#34923,#34924);
#29806=AXIS2_PLACEMENT_3D('',#148520,#34926,#34927);
#29807=AXIS2_PLACEMENT_3D('',#148790,#34929,#34930);
#29808=AXIS2_PLACEMENT_3D('',#149071,#34932,#34933);
#29809=AXIS2_PLACEMENT_3D('',#149402,#34935,#34936);
#29810=AXIS2_PLACEMENT_3D('',#149565,#34938,#34939);
#29811=AXIS2_PLACEMENT_3D('',#149831,#34941,#34942);
#29812=AXIS2_PLACEMENT_3D('',#150112,#34944,#34945);
#29813=AXIS2_PLACEMENT_3D('',#150445,#34947,#34948);
#29814=AXIS2_PLACEMENT_3D('',#150726,#34950,#34951);
#29815=AXIS2_PLACEMENT_3D('',#150824,#34953,#34954);
#29816=AXIS2_PLACEMENT_3D('',#150897,#34956,#34957);
#29817=AXIS2_PLACEMENT_3D('',#150912,#34958,#34959);
#29818=AXIS2_PLACEMENT_3D('',#151063,#34961,#34962);
#29819=AXIS2_PLACEMENT_3D('',#151396,#34964,#34965);
#29820=AXIS2_PLACEMENT_3D('',#151677,#34967,#34968);
#29821=AXIS2_PLACEMENT_3D('',#152013,#34970,#34971);
#29822=AXIS2_PLACEMENT_3D('',#152175,#34973,#34974);
#29823=AXIS2_PLACEMENT_3D('',#152445,#34976,#34977);
#29824=AXIS2_PLACEMENT_3D('',#152720,#34979,#34980);
#29825=AXIS2_PLACEMENT_3D('',#153054,#34982,#34983);
#29826=AXIS2_PLACEMENT_3D('',#153216,#34985,#34986);
#29827=AXIS2_PLACEMENT_3D('',#153483,#34988,#34989);
#29828=AXIS2_PLACEMENT_3D('',#153761,#34991,#34992);
#29829=AXIS2_PLACEMENT_3D('',#154094,#34994,#34995);
#29830=AXIS2_PLACEMENT_3D('',#154259,#34997,#34998);
#29831=AXIS2_PLACEMENT_3D('',#154528,#35000,#35001);
#29832=AXIS2_PLACEMENT_3D('',#154809,#35003,#35004);
#29833=AXIS2_PLACEMENT_3D('',#155142,#35006,#35007);
#29834=AXIS2_PLACEMENT_3D('',#155301,#35009,#35010);
#29835=AXIS2_PLACEMENT_3D('',#155571,#35012,#35013);
#29836=AXIS2_PLACEMENT_3D('',#155852,#35015,#35016);
#29837=AXIS2_PLACEMENT_3D('',#156183,#35018,#35019);
#29838=AXIS2_PLACEMENT_3D('',#156346,#35021,#35022);
#29839=AXIS2_PLACEMENT_3D('',#156612,#35024,#35025);
#29840=AXIS2_PLACEMENT_3D('',#156893,#35027,#35028);
#29841=AXIS2_PLACEMENT_3D('',#157226,#35030,#35031);
#29842=AXIS2_PLACEMENT_3D('',#157507,#35033,#35034);
#29843=AXIS2_PLACEMENT_3D('',#157605,#35036,#35037);
#29844=AXIS2_PLACEMENT_3D('',#157626,#35039,#35040);
#29845=AXIS2_PLACEMENT_3D('',#157627,#35041,#35042);
#29846=AXIS2_PLACEMENT_3D('',#157686,#35044,#35045);
#29847=AXIS2_PLACEMENT_3D('',#157739,#35046,#35047);
#29848=AXIS2_PLACEMENT_3D('',#158027,#35049,#35050);
#29849=AXIS2_PLACEMENT_3D('',#158313,#35052,#35053);
#29850=AXIS2_PLACEMENT_3D('',#158334,#35055,#35056);
#29851=AXIS2_PLACEMENT_3D('',#158369,#35057,#35058);
#29852=AXIS2_PLACEMENT_3D('',#158655,#35060,#35061);
#29853=AXIS2_PLACEMENT_3D('',#158945,#35063,#35064);
#29854=AXIS2_PLACEMENT_3D('',#158950,#35066,#35067);
#29855=AXIS2_PLACEMENT_3D('',#159057,#35068,#35069);
#29856=AXIS2_PLACEMENT_3D('',#159243,#35071,#35072);
#29857=AXIS2_PLACEMENT_3D('',#159389,#35073,#35074);
#29858=AXIS2_PLACEMENT_3D('',#159825,#35076,#35077);
#29859=AXIS2_PLACEMENT_3D('',#160284,#35079,#35080);
#29860=AXIS2_PLACEMENT_3D('',#160586,#35082,#35083);
#29861=AXIS2_PLACEMENT_3D('',#161058,#35085,#35086);
#29862=AXIS2_PLACEMENT_3D('',#161548,#35088,#35089);
#29863=AXIS2_PLACEMENT_3D('',#162066,#35091,#35092);
#29864=AXIS2_PLACEMENT_3D('',#162545,#35094,#35095);
#29865=AXIS2_PLACEMENT_3D('',#162964,#35097,#35098);
#29866=AXIS2_PLACEMENT_3D('',#163232,#35100,#35101);
#29867=AXIS2_PLACEMENT_3D('',#163690,#35103,#35104);
#29868=AXIS2_PLACEMENT_3D('',#164153,#35106,#35107);
#29869=AXIS2_PLACEMENT_3D('',#164453,#35109,#35110);
#29870=AXIS2_PLACEMENT_3D('',#164894,#35112,#35113);
#29871=AXIS2_PLACEMENT_3D('',#165317,#35115,#35116);
#29872=AXIS2_PLACEMENT_3D('',#165615,#35118,#35119);
#29873=AXIS2_PLACEMENT_3D('',#166079,#35121,#35122);
#29874=AXIS2_PLACEMENT_3D('',#166547,#35124,#35125);
#29875=AXIS2_PLACEMENT_3D('',#166790,#35127,#35128);
#29876=AXIS2_PLACEMENT_3D('',#167222,#35130,#35131);
#29877=AXIS2_PLACEMENT_3D('',#167690,#35133,#35134);
#29878=AXIS2_PLACEMENT_3D('',#168200,#35136,#35137);
#29879=AXIS2_PLACEMENT_3D('',#168670,#35139,#35140);
#29880=AXIS2_PLACEMENT_3D('',#169136,#35142,#35143);
#29881=AXIS2_PLACEMENT_3D('',#169435,#35145,#35146);
#29882=AXIS2_PLACEMENT_3D('',#169913,#35148,#35149);
#29883=AXIS2_PLACEMENT_3D('',#170348,#35151,#35152);
#29884=AXIS2_PLACEMENT_3D('',#170534,#35154,#35155);
#29885=AXIS2_PLACEMENT_3D('',#170680,#35156,#35157);
#29886=AXIS2_PLACEMENT_3D('',#171116,#35159,#35160);
#29887=AXIS2_PLACEMENT_3D('',#171571,#35162,#35163);
#29888=AXIS2_PLACEMENT_3D('',#171875,#35165,#35166);
#29889=AXIS2_PLACEMENT_3D('',#172347,#35168,#35169);
#29890=AXIS2_PLACEMENT_3D('',#172829,#35171,#35172);
#29891=AXIS2_PLACEMENT_3D('',#173335,#35174,#35175);
#29892=AXIS2_PLACEMENT_3D('',#173816,#35177,#35178);
#29893=AXIS2_PLACEMENT_3D('',#174281,#35180,#35181);
#29894=AXIS2_PLACEMENT_3D('',#174549,#35183,#35184);
#29895=AXIS2_PLACEMENT_3D('',#175007,#35186,#35187);
#29896=AXIS2_PLACEMENT_3D('',#175470,#35189,#35190);
#29897=AXIS2_PLACEMENT_3D('',#175770,#35192,#35193);
#29898=AXIS2_PLACEMENT_3D('',#176221,#35195,#35196);
#29899=AXIS2_PLACEMENT_3D('',#176646,#35198,#35199);
#29900=AXIS2_PLACEMENT_3D('',#176932,#35201,#35202);
#29901=AXIS2_PLACEMENT_3D('',#177400,#35204,#35205);
#29902=AXIS2_PLACEMENT_3D('',#177868,#35207,#35208);
#29903=AXIS2_PLACEMENT_3D('',#178111,#35210,#35211);
#29904=AXIS2_PLACEMENT_3D('',#178543,#35213,#35214);
#29905=AXIS2_PLACEMENT_3D('',#179013,#35216,#35217);
#29906=AXIS2_PLACEMENT_3D('',#179543,#35219,#35220);
#29907=AXIS2_PLACEMENT_3D('',#180013,#35222,#35223);
#29908=AXIS2_PLACEMENT_3D('',#180477,#35225,#35226);
#29909=AXIS2_PLACEMENT_3D('',#180746,#35228,#35229);
#29910=AXIS2_PLACEMENT_3D('',#181224,#35231,#35232);
#29911=AXIS2_PLACEMENT_3D('',#181659,#35234,#35235);
#29912=AXIS2_PLACEMENT_3D('',#181845,#35237,#35238);
#29913=AXIS2_PLACEMENT_3D('',#181991,#35239,#35240);
#29914=AXIS2_PLACEMENT_3D('',#182427,#35242,#35243);
#29915=AXIS2_PLACEMENT_3D('',#182886,#35245,#35246);
#29916=AXIS2_PLACEMENT_3D('',#183188,#35248,#35249);
#29917=AXIS2_PLACEMENT_3D('',#183648,#35251,#35252);
#29918=AXIS2_PLACEMENT_3D('',#184130,#35254,#35255);
#29919=AXIS2_PLACEMENT_3D('',#184640,#35257,#35258);
#29920=AXIS2_PLACEMENT_3D('',#185111,#35260,#35261);
#29921=AXIS2_PLACEMENT_3D('',#185534,#35263,#35264);
#29922=AXIS2_PLACEMENT_3D('',#185802,#35266,#35267);
#29923=AXIS2_PLACEMENT_3D('',#186262,#35269,#35270);
#29924=AXIS2_PLACEMENT_3D('',#186725,#35272,#35273);
#29925=AXIS2_PLACEMENT_3D('',#187049,#35275,#35276);
#29926=AXIS2_PLACEMENT_3D('',#187534,#35278,#35279);
#29927=AXIS2_PLACEMENT_3D('',#187995,#35281,#35282);
#29928=AXIS2_PLACEMENT_3D('',#188295,#35284,#35285);
#29929=AXIS2_PLACEMENT_3D('',#188759,#35287,#35288);
#29930=AXIS2_PLACEMENT_3D('',#189227,#35290,#35291);
#29931=AXIS2_PLACEMENT_3D('',#189470,#35293,#35294);
#29932=AXIS2_PLACEMENT_3D('',#189902,#35296,#35297);
#29933=AXIS2_PLACEMENT_3D('',#190378,#35299,#35300);
#29934=AXIS2_PLACEMENT_3D('',#190888,#35302,#35303);
#29935=AXIS2_PLACEMENT_3D('',#191362,#35305,#35306);
#29936=AXIS2_PLACEMENT_3D('',#191820,#35308,#35309);
#29937=AXIS2_PLACEMENT_3D('',#192075,#35311,#35312);
#29938=AXIS2_PLACEMENT_3D('',#192555,#35314,#35315);
#29939=AXIS2_PLACEMENT_3D('',#192990,#35317,#35318);
#29940=AXIS2_PLACEMENT_3D('',#193176,#35320,#35321);
#29941=AXIS2_PLACEMENT_3D('',#193322,#35322,#35323);
#29942=AXIS2_PLACEMENT_3D('',#193758,#35325,#35326);
#29943=AXIS2_PLACEMENT_3D('',#194215,#35328,#35329);
#29944=AXIS2_PLACEMENT_3D('',#194519,#35331,#35332);
#29945=AXIS2_PLACEMENT_3D('',#194981,#35334,#35335);
#29946=AXIS2_PLACEMENT_3D('',#195459,#35337,#35338);
#29947=AXIS2_PLACEMENT_3D('',#195951,#35340,#35341);
#29948=AXIS2_PLACEMENT_3D('',#196422,#35343,#35344);
#29949=AXIS2_PLACEMENT_3D('',#196891,#35346,#35347);
#29950=AXIS2_PLACEMENT_3D('',#197159,#35349,#35350);
#29951=AXIS2_PLACEMENT_3D('',#197625,#35352,#35353);
#29952=AXIS2_PLACEMENT_3D('',#198090,#35355,#35356);
#29953=AXIS2_PLACEMENT_3D('',#198388,#35358,#35359);
#29954=AXIS2_PLACEMENT_3D('',#198839,#35361,#35362);
#29955=AXIS2_PLACEMENT_3D('',#199264,#35364,#35365);
#29956=AXIS2_PLACEMENT_3D('',#199558,#35367,#35368);
#29957=AXIS2_PLACEMENT_3D('',#200024,#35370,#35371);
#29958=AXIS2_PLACEMENT_3D('',#200492,#35373,#35374);
#29959=AXIS2_PLACEMENT_3D('',#200735,#35376,#35377);
#29960=AXIS2_PLACEMENT_3D('',#201213,#35379,#35380);
#29961=AXIS2_PLACEMENT_3D('',#201691,#35382,#35383);
#29962=AXIS2_PLACEMENT_3D('',#202219,#35385,#35386);
#29963=AXIS2_PLACEMENT_3D('',#202693,#35388,#35389);
#29964=AXIS2_PLACEMENT_3D('',#203139,#35391,#35392);
#29965=AXIS2_PLACEMENT_3D('',#203436,#35394,#35395);
#29966=AXIS2_PLACEMENT_3D('',#203912,#35397,#35398);
#29967=AXIS2_PLACEMENT_3D('',#204347,#35400,#35401);
#29968=AXIS2_PLACEMENT_3D('',#204510,#35402,#35403);
#29969=AXIS2_PLACEMENT_3D('',#204617,#35404,#35405);
#29970=AXIS2_PLACEMENT_3D('',#204780,#35406,#35407);
#29971=AXIS2_PLACEMENT_3D('',#204887,#35408,#35409);
#29972=AXIS2_PLACEMENT_3D('',#205050,#35410,#35411);
#29973=AXIS2_PLACEMENT_3D('',#205157,#35412,#35413);
#29974=AXIS2_PLACEMENT_3D('',#205320,#35414,#35415);
#29975=AXIS2_PLACEMENT_3D('',#205427,#35416,#35417);
#29976=AXIS2_PLACEMENT_3D('',#205445,#35418,#35419);
#29977=AXIS2_PLACEMENT_3D('',#205446,#35420,#35421);
#29978=AXIS2_PLACEMENT_3D('',#205464,#35422,#35423);
#29979=AXIS2_PLACEMENT_3D('',#205499,#35424,#35425);
#29980=AXIS2_PLACEMENT_3D('',#205568,#35426,#35427);
#29981=AXIS2_PLACEMENT_3D('',#205581,#35428,#35429);
#29982=AXIS2_PLACEMENT_3D('',#205650,#35430,#35431);
#29983=AXIS2_PLACEMENT_3D('',#205663,#35432,#35433);
#29984=AXIS2_PLACEMENT_3D('',#205732,#35434,#35435);
#29985=AXIS2_PLACEMENT_3D('',#205745,#35436,#35437);
#29986=AXIS2_PLACEMENT_3D('',#205814,#35438,#35439);
#29987=AXIS2_PLACEMENT_3D('',#205827,#35440,#35441);
#29988=AXIS2_PLACEMENT_3D('',#205991,#35442,#35443);
#29989=AXIS2_PLACEMENT_3D('',#206047,#35444,#35445);
#29990=AXIS2_PLACEMENT_3D('',#206211,#35446,#35447);
#29991=AXIS2_PLACEMENT_3D('',#206267,#35448,#35449);
#29992=AXIS2_PLACEMENT_3D('',#206269,#35450,#35451);
#29993=AXIS2_PLACEMENT_3D('',#206272,#35453,#35454);
#29994=AXIS2_PLACEMENT_3D('',#206273,#35455,#35456);
#29995=AXIS2_PLACEMENT_3D('',#206274,#35457,#35458);
#29996=AXIS2_PLACEMENT_3D('',#206277,#35459,#35460);
#29997=AXIS2_PLACEMENT_3D('',#206281,#35462,#35463);
#29998=AXIS2_PLACEMENT_3D('',#206283,#35465,#35466);
#29999=AXIS2_PLACEMENT_3D('',#206287,#35468,#35469);
#30000=AXIS2_PLACEMENT_3D('',#206291,#35472,#35473);
#30001=AXIS2_PLACEMENT_3D('',#206293,#35474,#35475);
#30002=AXIS2_PLACEMENT_3D('',#206296,#35477,#35478);
#30003=AXIS2_PLACEMENT_3D('',#206297,#35479,#35480);
#30004=AXIS2_PLACEMENT_3D('',#206298,#35481,#35482);
#30005=AXIS2_PLACEMENT_3D('',#206301,#35483,#35484);
#30006=AXIS2_PLACEMENT_3D('',#206305,#35486,#35487);
#30007=AXIS2_PLACEMENT_3D('',#206307,#35489,#35490);
#30008=AXIS2_PLACEMENT_3D('',#206312,#35492,#35493);
#30009=AXIS2_PLACEMENT_3D('',#206315,#35496,#35497);
#30010=AXIS2_PLACEMENT_3D('',#206317,#35498,#35499);
#30011=AXIS2_PLACEMENT_3D('',#206320,#35501,#35502);
#30012=AXIS2_PLACEMENT_3D('',#206321,#35503,#35504);
#30013=AXIS2_PLACEMENT_3D('',#206322,#35505,#35506);
#30014=AXIS2_PLACEMENT_3D('',#206328,#35510,#35511);
#30015=AXIS2_PLACEMENT_3D('',#206336,#35516,#35517);
#30016=AXIS2_PLACEMENT_3D('',#206341,#35521,#35522);
#30017=AXIS2_PLACEMENT_3D('',#206343,#35523,#35524);
#30018=AXIS2_PLACEMENT_3D('',#206347,#35526,#35527);
#30019=AXIS2_PLACEMENT_3D('',#206351,#35529,#35530);
#30020=AXIS2_PLACEMENT_3D('',#206355,#35532,#35533);
#30021=AXIS2_PLACEMENT_3D('',#206367,#35539,#35540);
#30022=AXIS2_PLACEMENT_3D('',#206371,#35542,#35543);
#30023=AXIS2_PLACEMENT_3D('',#206383,#35549,#35550);
#30024=AXIS2_PLACEMENT_3D('',#206387,#35552,#35553);
#30025=AXIS2_PLACEMENT_3D('',#206391,#35555,#35556);
#30026=AXIS2_PLACEMENT_3D('',#206395,#35558,#35559);
#30027=AXIS2_PLACEMENT_3D('',#206398,#35561,#35562);
#30028=AXIS2_PLACEMENT_3D('',#206400,#35563,#35564);
#30029=AXIS2_PLACEMENT_3D('',#215196,#35565,#35566);
#30030=AXIS2_PLACEMENT_3D('',#215205,#35571,#35572);
#30031=AXIS2_PLACEMENT_3D('',#215211,#35576,#35577);
#30032=AXIS2_PLACEMENT_3D('',#215217,#35581,#35582);
#30033=AXIS2_PLACEMENT_3D('',#215223,#35586,#35587);
#30034=AXIS2_PLACEMENT_3D('',#215229,#35591,#35592);
#30035=AXIS2_PLACEMENT_3D('',#215235,#35596,#35597);
#30036=AXIS2_PLACEMENT_3D('',#215238,#35600,#35601);
#30037=AXIS2_PLACEMENT_3D('',#215240,#35602,#35603);
#30038=AXIS2_PLACEMENT_3D('',#215243,#35605,#35606);
#30039=AXIS2_PLACEMENT_3D('',#215244,#35607,#35608);
#30040=AXIS2_PLACEMENT_3D('',#215245,#35609,#35610);
#30041=AXIS2_PLACEMENT_3D('',#215248,#35611,#35612);
#30042=AXIS2_PLACEMENT_3D('',#215252,#35614,#35615);
#30043=AXIS2_PLACEMENT_3D('',#215254,#35617,#35618);
#30044=AXIS2_PLACEMENT_3D('',#215260,#35622,#35623);
#30045=AXIS2_PLACEMENT_3D('',#215262,#35624,#35625);
#30046=AXIS2_PLACEMENT_3D('',#215265,#35627,#35628);
#30047=AXIS2_PLACEMENT_3D('',#215266,#35629,#35630);
#30048=AXIS2_PLACEMENT_3D('',#215269,#35633,#35634);
#30049=AXIS2_PLACEMENT_3D('',#215272,#35637,#35638);
#30050=AXIS2_PLACEMENT_3D('',#215274,#35639,#35640);
#30051=AXIS2_PLACEMENT_3D('',#215276,#35641,#35642);
#30052=AXIS2_PLACEMENT_3D('',#215277,#35643,#35644);
#30053=AXIS2_PLACEMENT_3D('',#215286,#35649,#35650);
#30054=AXIS2_PLACEMENT_3D('',#215292,#35654,#35655);
#30055=AXIS2_PLACEMENT_3D('',#215298,#35659,#35660);
#30056=AXIS2_PLACEMENT_3D('',#215304,#35664,#35665);
#30057=AXIS2_PLACEMENT_3D('',#215310,#35669,#35670);
#30058=AXIS2_PLACEMENT_3D('',#215316,#35674,#35675);
#30059=AXIS2_PLACEMENT_3D('',#215319,#35678,#35679);
#30060=AXIS2_PLACEMENT_3D('',#215321,#35680,#35681);
#30061=AXIS2_PLACEMENT_3D('',#215324,#35683,#35684);
#30062=AXIS2_PLACEMENT_3D('',#215325,#35685,#35686);
#30063=AXIS2_PLACEMENT_3D('',#215326,#35687,#35688);
#30064=AXIS2_PLACEMENT_3D('',#215327,#35689,#35690);
#30065=AXIS2_PLACEMENT_3D('',#215328,#35691,#35692);
#30066=AXIS2_PLACEMENT_3D('',#215331,#35694,#35695);
#30067=AXIS2_PLACEMENT_3D('',#215332,#35696,#35697);
#30068=AXIS2_PLACEMENT_3D('',#215333,#35698,#35699);
#30069=AXIS2_PLACEMENT_3D('',#215334,#35700,#35701);
#30070=AXIS2_PLACEMENT_3D('',#215337,#35703,#35704);
#30071=AXIS2_PLACEMENT_3D('',#215338,#35705,#35706);
#30072=AXIS2_PLACEMENT_3D('',#215339,#35707,#35708);
#30073=AXIS2_PLACEMENT_3D('',#215342,#35709,#35710);
#30074=AXIS2_PLACEMENT_3D('',#215346,#35712,#35713);
#30075=AXIS2_PLACEMENT_3D('',#215348,#35715,#35716);
#30076=AXIS2_PLACEMENT_3D('',#215354,#35720,#35721);
#30077=AXIS2_PLACEMENT_3D('',#215356,#35722,#35723);
#30078=AXIS2_PLACEMENT_3D('',#215358,#35724,#35725);
#30079=AXIS2_PLACEMENT_3D('',#215360,#35727,#35728);
#30080=AXIS2_PLACEMENT_3D('',#215363,#35731,#35732);
#30081=AXIS2_PLACEMENT_3D('',#215366,#35735,#35736);
#30082=AXIS2_PLACEMENT_3D('',#215368,#35737,#35738);
#30083=AXIS2_PLACEMENT_3D('',#215370,#35739,#35740);
#30084=AXIS2_PLACEMENT_3D('',#215371,#35741,#35742);
#30085=AXIS2_PLACEMENT_3D('',#215380,#35747,#35748);
#30086=AXIS2_PLACEMENT_3D('',#215386,#35752,#35753);
#30087=AXIS2_PLACEMENT_3D('',#215392,#35757,#35758);
#30088=AXIS2_PLACEMENT_3D('',#215398,#35762,#35763);
#30089=AXIS2_PLACEMENT_3D('',#215404,#35767,#35768);
#30090=AXIS2_PLACEMENT_3D('',#215410,#35772,#35773);
#30091=AXIS2_PLACEMENT_3D('',#215413,#35776,#35777);
#30092=AXIS2_PLACEMENT_3D('',#215415,#35778,#35779);
#30093=AXIS2_PLACEMENT_3D('',#215418,#35781,#35782);
#30094=AXIS2_PLACEMENT_3D('',#215419,#35783,#35784);
#30095=AXIS2_PLACEMENT_3D('',#215420,#35785,#35786);
#30096=AXIS2_PLACEMENT_3D('',#215429,#35791,#35792);
#30097=AXIS2_PLACEMENT_3D('',#215435,#35796,#35797);
#30098=AXIS2_PLACEMENT_3D('',#215441,#35801,#35802);
#30099=AXIS2_PLACEMENT_3D('',#215447,#35806,#35807);
#30100=AXIS2_PLACEMENT_3D('',#215453,#35811,#35812);
#30101=AXIS2_PLACEMENT_3D('',#215459,#35816,#35817);
#30102=AXIS2_PLACEMENT_3D('',#215462,#35820,#35821);
#30103=AXIS2_PLACEMENT_3D('',#215464,#35822,#35823);
#30104=AXIS2_PLACEMENT_3D('',#215467,#35825,#35826);
#30105=AXIS2_PLACEMENT_3D('',#215468,#35827,#35828);
#30106=AXIS2_PLACEMENT_3D('',#215469,#35829,#35830);
#30107=AXIS2_PLACEMENT_3D('',#215470,#35831,#35832);
#30108=AXIS2_PLACEMENT_3D('',#215471,#35833,#35834);
#30109=AXIS2_PLACEMENT_3D('',#215477,#35838,#35839);
#30110=AXIS2_PLACEMENT_3D('',#215478,#35840,#35841);
#30111=AXIS2_PLACEMENT_3D('',#215480,#35842,#35843);
#30112=AXIS2_PLACEMENT_3D('',#215482,#35845,#35846);
#30113=AXIS2_PLACEMENT_3D('',#215483,#35847,#35848);
#30114=AXIS2_PLACEMENT_3D('',#215485,#35849,#35850);
#30115=AXIS2_PLACEMENT_3D('',#215487,#35852,#35853);
#30116=AXIS2_PLACEMENT_3D('',#215488,#35854,#35855);
#30117=AXIS2_PLACEMENT_3D('',#215490,#35856,#35857);
#30118=AXIS2_PLACEMENT_3D('',#215492,#35859,#35860);
#30119=AXIS2_PLACEMENT_3D('',#215493,#35861,#35862);
#30120=AXIS2_PLACEMENT_3D('',#215495,#35863,#35864);
#30121=AXIS2_PLACEMENT_3D('',#215497,#35866,#35867);
#30122=AXIS2_PLACEMENT_3D('',#215498,#35868,#35869);
#30123=AXIS2_PLACEMENT_3D('',#215502,#35872,#35873);
#30124=AXIS2_PLACEMENT_3D('',#215503,#35874,#35875);
#30125=AXIS2_PLACEMENT_3D('',#215504,#35876,#35877);
#30126=AXIS2_PLACEMENT_3D('',#215506,#35878,#35879);
#30127=AXIS2_PLACEMENT_3D('',#215508,#35881,#35882);
#30128=AXIS2_PLACEMENT_3D('',#215512,#35885,#35886);
#30129=AXIS2_PLACEMENT_3D('',#215514,#35887,#35888);
#30130=AXIS2_PLACEMENT_3D('',#215516,#35890,#35891);
#30131=AXIS2_PLACEMENT_3D('',#215520,#35894,#35895);
#30132=AXIS2_PLACEMENT_3D('',#215522,#35896,#35897);
#30133=AXIS2_PLACEMENT_3D('',#215524,#35899,#35900);
#30134=AXIS2_PLACEMENT_3D('',#215528,#35903,#35904);
#30135=AXIS2_PLACEMENT_3D('',#215529,#35905,#35906);
#30136=AXIS2_PLACEMENT_3D('',#215530,#35907,#35908);
#30137=AXIS2_PLACEMENT_3D('',#215532,#35909,#35910);
#30138=AXIS2_PLACEMENT_3D('',#215534,#35912,#35913);
#30139=AXIS2_PLACEMENT_3D('',#215538,#35916,#35917);
#30140=AXIS2_PLACEMENT_3D('',#215540,#35918,#35919);
#30141=AXIS2_PLACEMENT_3D('',#215542,#35921,#35922);
#30142=AXIS2_PLACEMENT_3D('',#215546,#35925,#35926);
#30143=AXIS2_PLACEMENT_3D('',#215548,#35927,#35928);
#30144=AXIS2_PLACEMENT_3D('',#215550,#35930,#35931);
#30145=AXIS2_PLACEMENT_3D('',#215554,#35934,#35935);
#30146=AXIS2_PLACEMENT_3D('',#215556,#35936,#35937);
#30147=AXIS2_PLACEMENT_3D('',#215558,#35939,#35940);
#30148=AXIS2_PLACEMENT_3D('',#215562,#35943,#35944);
#30149=AXIS2_PLACEMENT_3D('',#215564,#35945,#35946);
#30150=AXIS2_PLACEMENT_3D('',#215566,#35948,#35949);
#30151=AXIS2_PLACEMENT_3D('',#215570,#35952,#35953);
#30152=AXIS2_PLACEMENT_3D('',#215572,#35954,#35955);
#30153=AXIS2_PLACEMENT_3D('',#215574,#35957,#35958);
#30154=AXIS2_PLACEMENT_3D('',#215578,#35961,#35962);
#30155=AXIS2_PLACEMENT_3D('',#215579,#35963,#35964);
#30156=AXIS2_PLACEMENT_3D('',#215580,#35965,#35966);
#34674=DIRECTION('axis',(0.,0.,1.));
#34675=DIRECTION('refdir',(1.,0.,0.));
#34676=DIRECTION('center_axis',(-1.,0.,0.));
#34677=DIRECTION('ref_axis',(0.,0.878663232865503,-0.477442062673936));
#34678=DIRECTION('',(-1.,0.,0.));
#34679=DIRECTION('center_axis',(-1.,0.,0.));
#34680=DIRECTION('ref_axis',(0.,-1.74186785585433E-15,-1.));
#34681=DIRECTION('center_axis',(-1.,0.,0.));
#34682=DIRECTION('ref_axis',(0.,0.878663232865503,-0.477442062673936));
#34683=DIRECTION('',(-1.,0.,0.));
#34684=DIRECTION('center_axis',(-1.,0.,0.));
#34685=DIRECTION('ref_axis',(0.,0.878663232865503,-0.477442062673936));
#34686=DIRECTION('',(-1.,0.,0.));
#34687=DIRECTION('center_axis',(-1.,0.,0.));
#34688=DIRECTION('ref_axis',(0.,0.878663232865503,-0.477442062673936));
#34689=DIRECTION('',(-1.,0.,0.));
#34690=DIRECTION('center_axis',(1.,0.,0.));
#34691=DIRECTION('ref_axis',(0.,-0.878663231892279,-0.477442064465015));
#34692=DIRECTION('',(1.,0.,0.));
#34693=DIRECTION('center_axis',(1.,0.,0.));
#34694=DIRECTION('ref_axis',(0.,-1.74186785585433E-15,-1.));
#34695=DIRECTION('center_axis',(1.,0.,0.));
#34696=DIRECTION('ref_axis',(0.,-0.878663231892279,-0.477442064465015));
#34697=DIRECTION('',(1.,0.,0.));
#34698=DIRECTION('center_axis',(1.,0.,0.));
#34699=DIRECTION('ref_axis',(0.,-0.878663231892279,-0.477442064465015));
#34700=DIRECTION('',(1.,0.,0.));
#34701=DIRECTION('center_axis',(1.,0.,0.));
#34702=DIRECTION('ref_axis',(0.,-0.878663231892279,-0.477442064465015));
#34703=DIRECTION('',(1.,0.,0.));
#34704=DIRECTION('center_axis',(0.,0.,-1.));
#34705=DIRECTION('ref_axis',(-0.609193659724225,0.793021490851165,0.));
#34706=DIRECTION('',(0.,0.,-1.));
#34707=DIRECTION('center_axis',(0.,0.,-1.));
#34708=DIRECTION('ref_axis',(1.,8.06646416329218E-14,0.));
#34709=DIRECTION('center_axis',(0.,0.,-1.));
#34710=DIRECTION('ref_axis',(-0.609193659724225,0.793021490851165,0.));
#34711=DIRECTION('',(0.,0.,-1.));
#34712=DIRECTION('center_axis',(0.,0.,-1.));
#34713=DIRECTION('ref_axis',(-0.609193659724225,0.793021490851165,0.));
#34714=DIRECTION('',(0.,0.,-1.));
#34715=DIRECTION('center_axis',(0.,0.,-1.));
#34716=DIRECTION('ref_axis',(-0.609193659724225,0.793021490851165,0.));
#34717=DIRECTION('',(0.,0.,-1.));
#34718=DIRECTION('center_axis',(0.,0.,-1.));
#34719=DIRECTION('ref_axis',(-0.609193659724225,0.793021490851165,0.));
#34720=DIRECTION('',(0.,0.,-1.));
#34721=DIRECTION('center_axis',(0.,0.,-1.));
#34722=DIRECTION('ref_axis',(-0.609193659724225,0.793021490851165,0.));
#34723=DIRECTION('',(0.,0.,-1.));
#34724=DIRECTION('center_axis',(0.,0.,-1.));
#34725=DIRECTION('ref_axis',(-0.609193659724225,0.793021490851165,0.));
#34726=DIRECTION('',(0.,0.,-1.));
#34727=DIRECTION('center_axis',(0.,0.,-1.));
#34728=DIRECTION('ref_axis',(-0.609193659724225,0.793021490851165,0.));
#34729=DIRECTION('',(0.,0.,-1.));
#34730=DIRECTION('center_axis',(0.,0.,-1.));
#34731=DIRECTION('ref_axis',(-0.609193659724225,0.793021490851165,0.));
#34732=DIRECTION('',(0.,0.,-1.));
#34733=DIRECTION('center_axis',(0.,0.,-1.));
#34734=DIRECTION('ref_axis',(-0.609193659724225,0.793021490851165,0.));
#34735=DIRECTION('',(0.,0.,-1.));
#34736=DIRECTION('center_axis',(0.,0.,-1.));
#34737=DIRECTION('ref_axis',(-0.609193659724225,0.793021490851165,0.));
#34738=DIRECTION('',(0.,0.,-1.));
#34739=DIRECTION('center_axis',(0.,0.,-1.));
#34740=DIRECTION('ref_axis',(-0.609193659724225,0.793021490851165,0.));
#34741=DIRECTION('',(0.,0.,-1.));
#34742=DIRECTION('center_axis',(0.,0.,-1.));
#34743=DIRECTION('ref_axis',(-0.609193659724225,0.793021490851165,0.));
#34744=DIRECTION('',(0.,0.,-1.));
#34745=DIRECTION('center_axis',(0.,0.,-1.));
#34746=DIRECTION('ref_axis',(-0.609193659724225,0.793021490851165,0.));
#34747=DIRECTION('',(0.,0.,-1.));
#34748=DIRECTION('center_axis',(0.,0.,-1.));
#34749=DIRECTION('ref_axis',(-0.609193659724225,0.793021490851165,0.));
#34750=DIRECTION('',(0.,0.,-1.));
#34751=DIRECTION('center_axis',(0.,0.,-1.));
#34752=DIRECTION('ref_axis',(-0.609193659724225,0.793021490851165,0.));
#34753=DIRECTION('',(0.,0.,-1.));
#34754=DIRECTION('center_axis',(0.,0.,-1.));
#34755=DIRECTION('ref_axis',(-0.609193659724225,0.793021490851165,0.));
#34756=DIRECTION('',(0.,0.,-1.));
#34757=DIRECTION('center_axis',(0.,0.,-1.));
#34758=DIRECTION('ref_axis',(-0.609193659724225,0.793021490851165,0.));
#34759=DIRECTION('',(0.,0.,-1.));
#34760=DIRECTION('center_axis',(0.,0.,-1.));
#34761=DIRECTION('ref_axis',(-0.609193659724225,0.793021490851165,0.));
#34762=DIRECTION('',(0.,0.,-1.));
#34763=DIRECTION('center_axis',(0.,0.,-1.));
#34764=DIRECTION('ref_axis',(-0.609193659724225,0.793021490851165,0.));
#34765=DIRECTION('',(0.,0.,-1.));
#34766=DIRECTION('center_axis',(0.,0.,-1.));
#34767=DIRECTION('ref_axis',(-0.609193659724225,0.793021490851165,0.));
#34768=DIRECTION('',(0.,0.,-1.));
#34769=DIRECTION('center_axis',(0.,0.,-1.));
#34770=DIRECTION('ref_axis',(-0.609193659724225,0.793021490851165,0.));
#34771=DIRECTION('',(0.,0.,-1.));
#34772=DIRECTION('center_axis',(0.,0.,-1.));
#34773=DIRECTION('ref_axis',(-0.609193659724225,0.793021490851165,0.));
#34774=DIRECTION('',(0.,0.,-1.));
#34775=DIRECTION('center_axis',(0.,0.,-1.));
#34776=DIRECTION('ref_axis',(-0.609193659724225,0.793021490851165,0.));
#34777=DIRECTION('',(0.,0.,-1.));
#34778=DIRECTION('center_axis',(0.,0.,-1.));
#34779=DIRECTION('ref_axis',(-0.609193659724225,0.793021490851165,0.));
#34780=DIRECTION('',(0.,0.,-1.));
#34781=DIRECTION('center_axis',(0.,0.,-1.));
#34782=DIRECTION('ref_axis',(-0.609193659724225,0.793021490851165,0.));
#34783=DIRECTION('',(0.,0.,-1.));
#34784=DIRECTION('center_axis',(0.,0.,-1.));
#34785=DIRECTION('ref_axis',(-0.609193659724225,0.793021490851165,0.));
#34786=DIRECTION('',(0.,0.,-1.));
#34787=DIRECTION('center_axis',(0.,0.,-1.));
#34788=DIRECTION('ref_axis',(-0.609193645039877,0.793021502131581,0.));
#34789=DIRECTION('',(0.,0.,-1.));
#34790=DIRECTION('center_axis',(0.,0.,-1.));
#34791=DIRECTION('ref_axis',(1.,8.15320033709099E-14,0.));
#34792=DIRECTION('center_axis',(0.,0.,-1.));
#34793=DIRECTION('ref_axis',(-0.609193645039877,0.793021502131581,0.));
#34794=DIRECTION('',(0.,0.,-1.));
#34795=DIRECTION('center_axis',(0.,0.,-1.));
#34796=DIRECTION('ref_axis',(-0.609193645039877,0.793021502131581,0.));
#34797=DIRECTION('',(0.,0.,-1.));
#34798=DIRECTION('center_axis',(0.,0.,-1.));
#34799=DIRECTION('ref_axis',(-0.609193645039877,0.793021502131581,0.));
#34800=DIRECTION('',(0.,0.,-1.));
#34801=DIRECTION('center_axis',(0.,0.,-1.));
#34802=DIRECTION('ref_axis',(-0.609193645039877,0.793021502131581,0.));
#34803=DIRECTION('',(0.,0.,-1.));
#34804=DIRECTION('center_axis',(0.,0.,-1.));
#34805=DIRECTION('ref_axis',(-0.609193645039877,0.793021502131581,0.));
#34806=DIRECTION('',(0.,0.,-1.));
#34807=DIRECTION('center_axis',(0.,0.,-1.));
#34808=DIRECTION('ref_axis',(-0.609193645039877,0.793021502131581,0.));
#34809=DIRECTION('',(0.,0.,-1.));
#34810=DIRECTION('center_axis',(0.,0.,-1.));
#34811=DIRECTION('ref_axis',(-0.609193645039877,0.793021502131581,0.));
#34812=DIRECTION('',(0.,0.,-1.));
#34813=DIRECTION('center_axis',(0.,0.,-1.));
#34814=DIRECTION('ref_axis',(-0.609193645039877,0.793021502131581,0.));
#34815=DIRECTION('',(0.,0.,-1.));
#34816=DIRECTION('center_axis',(0.,0.,-1.));
#34817=DIRECTION('ref_axis',(-0.609193645039877,0.793021502131581,0.));
#34818=DIRECTION('',(0.,0.,-1.));
#34819=DIRECTION('center_axis',(0.,0.,-1.));
#34820=DIRECTION('ref_axis',(-0.609193645039877,0.793021502131581,0.));
#34821=DIRECTION('',(0.,0.,-1.));
#34822=DIRECTION('center_axis',(0.,0.,-1.));
#34823=DIRECTION('ref_axis',(-0.609193645039877,0.793021502131581,0.));
#34824=DIRECTION('',(0.,0.,-1.));
#34825=DIRECTION('center_axis',(0.,0.,-1.));
#34826=DIRECTION('ref_axis',(-0.609193645039877,0.793021502131581,0.));
#34827=DIRECTION('',(0.,0.,-1.));
#34828=DIRECTION('center_axis',(0.,0.,-1.));
#34829=DIRECTION('ref_axis',(-0.609193645039877,0.793021502131581,0.));
#34830=DIRECTION('',(0.,0.,-1.));
#34831=DIRECTION('center_axis',(0.,0.,-1.));
#34832=DIRECTION('ref_axis',(-0.609193645039877,0.793021502131581,0.));
#34833=DIRECTION('',(0.,0.,-1.));
#34834=DIRECTION('center_axis',(0.,0.,-1.));
#34835=DIRECTION('ref_axis',(-0.609193645039877,0.793021502131581,0.));
#34836=DIRECTION('',(0.,0.,-1.));
#34837=DIRECTION('center_axis',(0.,0.,-1.));
#34838=DIRECTION('ref_axis',(-0.609193645039877,0.793021502131581,0.));
#34839=DIRECTION('',(0.,0.,-1.));
#34840=DIRECTION('center_axis',(0.,0.,-1.));
#34841=DIRECTION('ref_axis',(-0.609193645039877,0.793021502131581,0.));
#34842=DIRECTION('',(0.,0.,-1.));
#34843=DIRECTION('center_axis',(0.,0.,-1.));
#34844=DIRECTION('ref_axis',(-0.609193645039877,0.793021502131581,0.));
#34845=DIRECTION('',(0.,0.,-1.));
#34846=DIRECTION('center_axis',(0.,0.,-1.));
#34847=DIRECTION('ref_axis',(-0.609193645039877,0.793021502131581,0.));
#34848=DIRECTION('',(0.,0.,-1.));
#34849=DIRECTION('center_axis',(0.,0.,-1.));
#34850=DIRECTION('ref_axis',(-0.609193645039877,0.793021502131581,0.));
#34851=DIRECTION('',(0.,0.,-1.));
#34852=DIRECTION('center_axis',(0.,0.,-1.));
#34853=DIRECTION('ref_axis',(-0.609193645039877,0.793021502131581,0.));
#34854=DIRECTION('',(0.,0.,-1.));
#34855=DIRECTION('center_axis',(0.,0.,-1.));
#34856=DIRECTION('ref_axis',(-0.609193645039877,0.793021502131581,0.));
#34857=DIRECTION('',(0.,0.,-1.));
#34858=DIRECTION('center_axis',(0.,0.,-1.));
#34859=DIRECTION('ref_axis',(-0.609193645039877,0.793021502131581,0.));
#34860=DIRECTION('',(0.,0.,-1.));
#34861=DIRECTION('center_axis',(0.,0.,-1.));
#34862=DIRECTION('ref_axis',(-0.609193645039877,0.793021502131581,0.));
#34863=DIRECTION('',(0.,0.,-1.));
#34864=DIRECTION('center_axis',(0.,0.,-1.));
#34865=DIRECTION('ref_axis',(-0.609193645039877,0.793021502131581,0.));
#34866=DIRECTION('',(0.,0.,-1.));
#34867=DIRECTION('center_axis',(0.,0.,-1.));
#34868=DIRECTION('ref_axis',(-0.609193645039877,0.793021502131581,0.));
#34869=DIRECTION('',(0.,0.,-1.));
#34870=DIRECTION('center_axis',(0.,0.,-1.));
#34871=DIRECTION('ref_axis',(-0.609193651103488,0.793021497473556,0.));
#34872=DIRECTION('',(0.,0.,-1.));
#34873=DIRECTION('center_axis',(0.,0.,-1.));
#34874=DIRECTION('ref_axis',(1.,7.80625564189563E-14,0.));
#34875=DIRECTION('center_axis',(0.,0.,-1.));
#34876=DIRECTION('ref_axis',(-0.609193651103488,0.793021497473556,0.));
#34877=DIRECTION('',(0.,0.,-1.));
#34878=DIRECTION('center_axis',(0.,0.,-1.));
#34879=DIRECTION('ref_axis',(-0.609193651103488,0.793021497473556,0.));
#34880=DIRECTION('',(0.,0.,-1.));
#34881=DIRECTION('center_axis',(0.,0.,-1.));
#34882=DIRECTION('ref_axis',(-0.609193651103488,0.793021497473556,0.));
#34883=DIRECTION('',(0.,0.,-1.));
#34884=DIRECTION('center_axis',(0.,0.,-1.));
#34885=DIRECTION('ref_axis',(-0.609193651103488,0.793021497473556,0.));
#34886=DIRECTION('',(0.,0.,-1.));
#34887=DIRECTION('center_axis',(0.,0.,-1.));
#34888=DIRECTION('ref_axis',(-0.609193651103488,0.793021497473556,0.));
#34889=DIRECTION('',(0.,0.,-1.));
#34890=DIRECTION('center_axis',(0.,0.,-1.));
#34891=DIRECTION('ref_axis',(-0.609193651103488,0.793021497473556,0.));
#34892=DIRECTION('',(0.,0.,-1.));
#34893=DIRECTION('center_axis',(0.,0.,-1.));
#34894=DIRECTION('ref_axis',(-0.609193651103488,0.793021497473556,0.));
#34895=DIRECTION('',(0.,0.,-1.));
#34896=DIRECTION('center_axis',(0.,0.,-1.));
#34897=DIRECTION('ref_axis',(-0.609193651103488,0.793021497473556,0.));
#34898=DIRECTION('',(0.,0.,-1.));
#34899=DIRECTION('center_axis',(0.,0.,-1.));
#34900=DIRECTION('ref_axis',(-0.609193651103488,0.793021497473556,0.));
#34901=DIRECTION('',(0.,0.,-1.));
#34902=DIRECTION('center_axis',(0.,0.,-1.));
#34903=DIRECTION('ref_axis',(-0.609193651103488,0.793021497473556,0.));
#34904=DIRECTION('',(0.,0.,-1.));
#34905=DIRECTION('center_axis',(0.,0.,-1.));
#34906=DIRECTION('ref_axis',(-0.609193651103488,0.793021497473556,0.));
#34907=DIRECTION('',(0.,0.,-1.));
#34908=DIRECTION('center_axis',(0.,0.,-1.));
#34909=DIRECTION('ref_axis',(-0.609193651103488,0.793021497473556,0.));
#34910=DIRECTION('',(0.,0.,-1.));
#34911=DIRECTION('center_axis',(0.,0.,-1.));
#34912=DIRECTION('ref_axis',(-0.609193651103488,0.793021497473556,0.));
#34913=DIRECTION('',(0.,0.,-1.));
#34914=DIRECTION('center_axis',(0.,0.,-1.));
#34915=DIRECTION('ref_axis',(-0.609193651103488,0.793021497473556,0.));
#34916=DIRECTION('',(0.,0.,-1.));
#34917=DIRECTION('center_axis',(0.,0.,-1.));
#34918=DIRECTION('ref_axis',(-0.609193651103488,0.793021497473556,0.));
#34919=DIRECTION('',(0.,0.,-1.));
#34920=DIRECTION('center_axis',(0.,0.,-1.));
#34921=DIRECTION('ref_axis',(-0.609193651103488,0.793021497473556,0.));
#34922=DIRECTION('',(0.,0.,-1.));
#34923=DIRECTION('center_axis',(0.,0.,-1.));
#34924=DIRECTION('ref_axis',(-0.609193651103488,0.793021497473556,0.));
#34925=DIRECTION('',(0.,0.,-1.));
#34926=DIRECTION('center_axis',(0.,0.,-1.));
#34927=DIRECTION('ref_axis',(-0.609193651103488,0.793021497473556,0.));
#34928=DIRECTION('',(0.,0.,-1.));
#34929=DIRECTION('center_axis',(0.,0.,-1.));
#34930=DIRECTION('ref_axis',(-0.609193651103488,0.793021497473556,0.));
#34931=DIRECTION('',(0.,0.,-1.));
#34932=DIRECTION('center_axis',(0.,0.,-1.));
#34933=DIRECTION('ref_axis',(-0.609193651103488,0.793021497473556,0.));
#34934=DIRECTION('',(0.,0.,-1.));
#34935=DIRECTION('center_axis',(0.,0.,-1.));
#34936=DIRECTION('ref_axis',(-0.609193651103488,0.793021497473556,0.));
#34937=DIRECTION('',(0.,0.,-1.));
#34938=DIRECTION('center_axis',(0.,0.,-1.));
#34939=DIRECTION('ref_axis',(-0.609193651103488,0.793021497473556,0.));
#34940=DIRECTION('',(0.,0.,-1.));
#34941=DIRECTION('center_axis',(0.,0.,-1.));
#34942=DIRECTION('ref_axis',(-0.609193651103488,0.793021497473556,0.));
#34943=DIRECTION('',(0.,0.,-1.));
#34944=DIRECTION('center_axis',(0.,0.,-1.));
#34945=DIRECTION('ref_axis',(-0.609193651103488,0.793021497473556,0.));
#34946=DIRECTION('',(0.,0.,-1.));
#34947=DIRECTION('center_axis',(0.,0.,-1.));
#34948=DIRECTION('ref_axis',(-0.609193651103488,0.793021497473556,0.));
#34949=DIRECTION('',(0.,0.,-1.));
#34950=DIRECTION('center_axis',(0.,0.,-1.));
#34951=DIRECTION('ref_axis',(-0.609193651103488,0.793021497473556,0.));
#34952=DIRECTION('',(0.,0.,-1.));
#34953=DIRECTION('center_axis',(0.,0.,-1.));
#34954=DIRECTION('ref_axis',(-0.609193695218696,0.793021463584555,0.));
#34955=DIRECTION('',(0.,0.,-1.));
#34956=DIRECTION('center_axis',(0.,0.,-1.));
#34957=DIRECTION('ref_axis',(1.,7.89299181569448E-14,0.));
#34958=DIRECTION('center_axis',(0.,0.,-1.));
#34959=DIRECTION('ref_axis',(-0.609193695218696,0.793021463584555,0.));
#34960=DIRECTION('',(0.,0.,-1.));
#34961=DIRECTION('center_axis',(0.,0.,-1.));
#34962=DIRECTION('ref_axis',(-0.609193695218696,0.793021463584555,0.));
#34963=DIRECTION('',(0.,0.,-1.));
#34964=DIRECTION('center_axis',(0.,0.,-1.));
#34965=DIRECTION('ref_axis',(-0.609193695218696,0.793021463584555,0.));
#34966=DIRECTION('',(0.,0.,-1.));
#34967=DIRECTION('center_axis',(0.,0.,-1.));
#34968=DIRECTION('ref_axis',(-0.609193695218696,0.793021463584555,0.));
#34969=DIRECTION('',(0.,0.,-1.));
#34970=DIRECTION('center_axis',(0.,0.,-1.));
#34971=DIRECTION('ref_axis',(-0.609193695218696,0.793021463584555,0.));
#34972=DIRECTION('',(0.,0.,-1.));
#34973=DIRECTION('center_axis',(0.,0.,-1.));
#34974=DIRECTION('ref_axis',(-0.609193695218696,0.793021463584555,0.));
#34975=DIRECTION('',(0.,0.,-1.));
#34976=DIRECTION('center_axis',(0.,0.,-1.));
#34977=DIRECTION('ref_axis',(-0.609193695218696,0.793021463584555,0.));
#34978=DIRECTION('',(0.,0.,-1.));
#34979=DIRECTION('center_axis',(0.,0.,-1.));
#34980=DIRECTION('ref_axis',(-0.609193695218696,0.793021463584555,0.));
#34981=DIRECTION('',(0.,0.,-1.));
#34982=DIRECTION('center_axis',(0.,0.,-1.));
#34983=DIRECTION('ref_axis',(-0.609193695218696,0.793021463584555,0.));
#34984=DIRECTION('',(0.,0.,-1.));
#34985=DIRECTION('center_axis',(0.,0.,-1.));
#34986=DIRECTION('ref_axis',(-0.609193695218696,0.793021463584555,0.));
#34987=DIRECTION('',(0.,0.,-1.));
#34988=DIRECTION('center_axis',(0.,0.,-1.));
#34989=DIRECTION('ref_axis',(-0.609193695218696,0.793021463584555,0.));
#34990=DIRECTION('',(0.,0.,-1.));
#34991=DIRECTION('center_axis',(0.,0.,-1.));
#34992=DIRECTION('ref_axis',(-0.609193695218696,0.793021463584555,0.));
#34993=DIRECTION('',(0.,0.,-1.));
#34994=DIRECTION('center_axis',(0.,0.,-1.));
#34995=DIRECTION('ref_axis',(-0.609193695218696,0.793021463584555,0.));
#34996=DIRECTION('',(0.,0.,-1.));
#34997=DIRECTION('center_axis',(0.,0.,-1.));
#34998=DIRECTION('ref_axis',(-0.609193695218696,0.793021463584555,0.));
#34999=DIRECTION('',(0.,0.,-1.));
#35000=DIRECTION('center_axis',(0.,0.,-1.));
#35001=DIRECTION('ref_axis',(-0.609193695218696,0.793021463584555,0.));
#35002=DIRECTION('',(0.,0.,-1.));
#35003=DIRECTION('center_axis',(0.,0.,-1.));
#35004=DIRECTION('ref_axis',(-0.609193695218696,0.793021463584555,0.));
#35005=DIRECTION('',(0.,0.,-1.));
#35006=DIRECTION('center_axis',(0.,0.,-1.));
#35007=DIRECTION('ref_axis',(-0.609193695218696,0.793021463584555,0.));
#35008=DIRECTION('',(0.,0.,-1.));
#35009=DIRECTION('center_axis',(0.,0.,-1.));
#35010=DIRECTION('ref_axis',(-0.609193695218696,0.793021463584555,0.));
#35011=DIRECTION('',(0.,0.,-1.));
#35012=DIRECTION('center_axis',(0.,0.,-1.));
#35013=DIRECTION('ref_axis',(-0.609193695218696,0.793021463584555,0.));
#35014=DIRECTION('',(0.,0.,-1.));
#35015=DIRECTION('center_axis',(0.,0.,-1.));
#35016=DIRECTION('ref_axis',(-0.609193695218696,0.793021463584555,0.));
#35017=DIRECTION('',(0.,0.,-1.));
#35018=DIRECTION('center_axis',(0.,0.,-1.));
#35019=DIRECTION('ref_axis',(-0.609193695218696,0.793021463584555,0.));
#35020=DIRECTION('',(0.,0.,-1.));
#35021=DIRECTION('center_axis',(0.,0.,-1.));
#35022=DIRECTION('ref_axis',(-0.609193695218696,0.793021463584555,0.));
#35023=DIRECTION('',(0.,0.,-1.));
#35024=DIRECTION('center_axis',(0.,0.,-1.));
#35025=DIRECTION('ref_axis',(-0.609193695218696,0.793021463584555,0.));
#35026=DIRECTION('',(0.,0.,-1.));
#35027=DIRECTION('center_axis',(0.,0.,-1.));
#35028=DIRECTION('ref_axis',(-0.609193695218696,0.793021463584555,0.));
#35029=DIRECTION('',(0.,0.,-1.));
#35030=DIRECTION('center_axis',(0.,0.,-1.));
#35031=DIRECTION('ref_axis',(-0.609193695218696,0.793021463584555,0.));
#35032=DIRECTION('',(0.,0.,-1.));
#35033=DIRECTION('center_axis',(0.,0.,-1.));
#35034=DIRECTION('ref_axis',(-0.609193695218696,0.793021463584555,0.));
#35035=DIRECTION('',(0.,0.,-1.));
#35036=DIRECTION('center_axis',(-1.,0.,0.));
#35037=DIRECTION('ref_axis',(0.,0.,-1.));
#35038=DIRECTION('',(-1.,0.,0.));
#35039=DIRECTION('center_axis',(1.,0.,0.));
#35040=DIRECTION('ref_axis',(0.,0.,-1.));
#35041=DIRECTION('center_axis',(-1.,0.,0.));
#35042=DIRECTION('ref_axis',(0.,0.,-1.));
#35043=DIRECTION('',(-1.,0.,0.));
#35044=DIRECTION('center_axis',(1.,0.,0.));
#35045=DIRECTION('ref_axis',(0.,0.,-1.));
#35046=DIRECTION('center_axis',(-1.,0.,0.));
#35047=DIRECTION('ref_axis',(0.,0.,-1.));
#35048=DIRECTION('',(-1.,0.,0.));
#35049=DIRECTION('center_axis',(-1.,0.,0.));
#35050=DIRECTION('ref_axis',(0.,0.,-1.));
#35051=DIRECTION('',(-1.,0.,0.));
#35052=DIRECTION('center_axis',(-1.,0.,0.));
#35053=DIRECTION('ref_axis',(0.,0.,-1.));
#35054=DIRECTION('',(-1.,0.,0.));
#35055=DIRECTION('center_axis',(-1.,0.,0.));
#35056=DIRECTION('ref_axis',(0.,0.,-1.));
#35057=DIRECTION('center_axis',(-1.,0.,0.));
#35058=DIRECTION('ref_axis',(0.,0.,-1.));
#35059=DIRECTION('',(-1.,0.,0.));
#35060=DIRECTION('center_axis',(-1.,0.,0.));
#35061=DIRECTION('ref_axis',(0.,0.,-1.));
#35062=DIRECTION('',(-1.,0.,0.));
#35063=DIRECTION('center_axis',(-1.,0.,0.));
#35064=DIRECTION('ref_axis',(0.,0.,-1.));
#35065=DIRECTION('',(-1.,0.,0.));
#35066=DIRECTION('center_axis',(-1.,0.,0.));
#35067=DIRECTION('ref_axis',(0.,0.,-1.));
#35068=DIRECTION('center_axis',(0.,0.,-1.));
#35069=DIRECTION('ref_axis',(0.939338957847042,-0.34299026556279,0.));
#35070=DIRECTION('',(0.,0.,-1.));
#35071=DIRECTION('center_axis',(0.,0.,1.));
#35072=DIRECTION('ref_axis',(1.,0.,0.));
#35073=DIRECTION('center_axis',(0.,0.,-1.));
#35074=DIRECTION('ref_axis',(0.939338957847042,-0.34299026556279,0.));
#35075=DIRECTION('',(0.,0.,-1.));
#35076=DIRECTION('center_axis',(0.,0.,-1.));
#35077=DIRECTION('ref_axis',(0.939338957847042,-0.34299026556279,0.));
#35078=DIRECTION('',(0.,0.,-1.));
#35079=DIRECTION('center_axis',(0.,0.,-1.));
#35080=DIRECTION('ref_axis',(0.939338957847042,-0.34299026556279,0.));
#35081=DIRECTION('',(0.,0.,-1.));
#35082=DIRECTION('center_axis',(0.,0.,-1.));
#35083=DIRECTION('ref_axis',(0.939338957847042,-0.34299026556279,0.));
#35084=DIRECTION('',(0.,0.,-1.));
#35085=DIRECTION('center_axis',(0.,0.,-1.));
#35086=DIRECTION('ref_axis',(0.939338957847042,-0.34299026556279,0.));
#35087=DIRECTION('',(0.,0.,-1.));
#35088=DIRECTION('center_axis',(0.,0.,-1.));
#35089=DIRECTION('ref_axis',(0.939338957847042,-0.34299026556279,0.));
#35090=DIRECTION('',(0.,0.,-1.));
#35091=DIRECTION('center_axis',(0.,0.,-1.));
#35092=DIRECTION('ref_axis',(0.939338957847042,-0.34299026556279,0.));
#35093=DIRECTION('',(0.,0.,-1.));
#35094=DIRECTION('center_axis',(0.,0.,-1.));
#35095=DIRECTION('ref_axis',(0.939338957847042,-0.34299026556279,0.));
#35096=DIRECTION('',(0.,0.,-1.));
#35097=DIRECTION('center_axis',(0.,0.,-1.));
#35098=DIRECTION('ref_axis',(0.939338957847042,-0.34299026556279,0.));
#35099=DIRECTION('',(0.,0.,-1.));
#35100=DIRECTION('center_axis',(0.,0.,-1.));
#35101=DIRECTION('ref_axis',(0.939338957847042,-0.34299026556279,0.));
#35102=DIRECTION('',(0.,0.,-1.));
#35103=DIRECTION('center_axis',(0.,0.,-1.));
#35104=DIRECTION('ref_axis',(0.939338957847042,-0.34299026556279,0.));
#35105=DIRECTION('',(0.,0.,-1.));
#35106=DIRECTION('center_axis',(0.,0.,-1.));
#35107=DIRECTION('ref_axis',(0.939338957847042,-0.34299026556279,0.));
#35108=DIRECTION('',(0.,0.,-1.));
#35109=DIRECTION('center_axis',(0.,0.,-1.));
#35110=DIRECTION('ref_axis',(0.939338957847042,-0.34299026556279,0.));
#35111=DIRECTION('',(0.,0.,-1.));
#35112=DIRECTION('center_axis',(0.,0.,-1.));
#35113=DIRECTION('ref_axis',(0.939338957847042,-0.34299026556279,0.));
#35114=DIRECTION('',(0.,0.,-1.));
#35115=DIRECTION('center_axis',(0.,0.,-1.));
#35116=DIRECTION('ref_axis',(0.939338957847042,-0.34299026556279,0.));
#35117=DIRECTION('',(0.,0.,-1.));
#35118=DIRECTION('center_axis',(0.,0.,-1.));
#35119=DIRECTION('ref_axis',(0.939338957847042,-0.34299026556279,0.));
#35120=DIRECTION('',(0.,0.,-1.));
#35121=DIRECTION('center_axis',(0.,0.,-1.));
#35122=DIRECTION('ref_axis',(0.939338957847042,-0.34299026556279,0.));
#35123=DIRECTION('',(0.,0.,-1.));
#35124=DIRECTION('center_axis',(0.,0.,-1.));
#35125=DIRECTION('ref_axis',(0.939338957847042,-0.34299026556279,0.));
#35126=DIRECTION('',(0.,0.,-1.));
#35127=DIRECTION('center_axis',(0.,0.,-1.));
#35128=DIRECTION('ref_axis',(0.939338957847042,-0.34299026556279,0.));
#35129=DIRECTION('',(0.,0.,-1.));
#35130=DIRECTION('center_axis',(0.,0.,-1.));
#35131=DIRECTION('ref_axis',(0.939338957847042,-0.34299026556279,0.));
#35132=DIRECTION('',(0.,0.,-1.));
#35133=DIRECTION('center_axis',(0.,0.,-1.));
#35134=DIRECTION('ref_axis',(0.939338957847042,-0.34299026556279,0.));
#35135=DIRECTION('',(0.,0.,-1.));
#35136=DIRECTION('center_axis',(0.,0.,-1.));
#35137=DIRECTION('ref_axis',(0.939338957847042,-0.34299026556279,0.));
#35138=DIRECTION('',(0.,0.,-1.));
#35139=DIRECTION('center_axis',(0.,0.,-1.));
#35140=DIRECTION('ref_axis',(0.939338957847042,-0.34299026556279,0.));
#35141=DIRECTION('',(0.,0.,-1.));
#35142=DIRECTION('center_axis',(0.,0.,-1.));
#35143=DIRECTION('ref_axis',(0.939338957847042,-0.34299026556279,0.));
#35144=DIRECTION('',(0.,0.,-1.));
#35145=DIRECTION('center_axis',(0.,0.,-1.));
#35146=DIRECTION('ref_axis',(0.939338957847042,-0.34299026556279,0.));
#35147=DIRECTION('',(0.,0.,-1.));
#35148=DIRECTION('center_axis',(0.,0.,-1.));
#35149=DIRECTION('ref_axis',(0.939338957847042,-0.34299026556279,0.));
#35150=DIRECTION('',(0.,0.,-1.));
#35151=DIRECTION('center_axis',(0.,0.,-1.));
#35152=DIRECTION('ref_axis',(0.939338984774712,-0.342990191816636,0.));
#35153=DIRECTION('',(0.,0.,-1.));
#35154=DIRECTION('center_axis',(0.,0.,1.));
#35155=DIRECTION('ref_axis',(1.,0.,0.));
#35156=DIRECTION('center_axis',(0.,0.,-1.));
#35157=DIRECTION('ref_axis',(0.939338984774712,-0.342990191816636,0.));
#35158=DIRECTION('',(0.,0.,-1.));
#35159=DIRECTION('center_axis',(0.,0.,-1.));
#35160=DIRECTION('ref_axis',(0.939338984774712,-0.342990191816636,0.));
#35161=DIRECTION('',(0.,0.,-1.));
#35162=DIRECTION('center_axis',(0.,0.,-1.));
#35163=DIRECTION('ref_axis',(0.939338984774712,-0.342990191816636,0.));
#35164=DIRECTION('',(0.,0.,-1.));
#35165=DIRECTION('center_axis',(0.,0.,-1.));
#35166=DIRECTION('ref_axis',(0.939338984774712,-0.342990191816636,0.));
#35167=DIRECTION('',(0.,0.,-1.));
#35168=DIRECTION('center_axis',(0.,0.,-1.));
#35169=DIRECTION('ref_axis',(0.939338984774712,-0.342990191816636,0.));
#35170=DIRECTION('',(0.,0.,-1.));
#35171=DIRECTION('center_axis',(0.,0.,-1.));
#35172=DIRECTION('ref_axis',(0.939338984774712,-0.342990191816636,0.));
#35173=DIRECTION('',(0.,0.,-1.));
#35174=DIRECTION('center_axis',(0.,0.,-1.));
#35175=DIRECTION('ref_axis',(0.939338984774712,-0.342990191816636,0.));
#35176=DIRECTION('',(0.,0.,-1.));
#35177=DIRECTION('center_axis',(0.,0.,-1.));
#35178=DIRECTION('ref_axis',(0.939338984774712,-0.342990191816636,0.));
#35179=DIRECTION('',(0.,0.,-1.));
#35180=DIRECTION('center_axis',(0.,0.,-1.));
#35181=DIRECTION('ref_axis',(0.939338984774712,-0.342990191816636,0.));
#35182=DIRECTION('',(0.,0.,-1.));
#35183=DIRECTION('center_axis',(0.,0.,-1.));
#35184=DIRECTION('ref_axis',(0.939338984774712,-0.342990191816636,0.));
#35185=DIRECTION('',(0.,0.,-1.));
#35186=DIRECTION('center_axis',(0.,0.,-1.));
#35187=DIRECTION('ref_axis',(0.939338984774712,-0.342990191816636,0.));
#35188=DIRECTION('',(0.,0.,-1.));
#35189=DIRECTION('center_axis',(0.,0.,-1.));
#35190=DIRECTION('ref_axis',(0.939338984774712,-0.342990191816636,0.));
#35191=DIRECTION('',(0.,0.,-1.));
#35192=DIRECTION('center_axis',(0.,0.,-1.));
#35193=DIRECTION('ref_axis',(0.939338984774712,-0.342990191816636,0.));
#35194=DIRECTION('',(0.,0.,-1.));
#35195=DIRECTION('center_axis',(0.,0.,-1.));
#35196=DIRECTION('ref_axis',(0.939338984774712,-0.342990191816636,0.));
#35197=DIRECTION('',(0.,0.,-1.));
#35198=DIRECTION('center_axis',(0.,0.,-1.));
#35199=DIRECTION('ref_axis',(0.939338984774712,-0.342990191816636,0.));
#35200=DIRECTION('',(0.,0.,-1.));
#35201=DIRECTION('center_axis',(0.,0.,-1.));
#35202=DIRECTION('ref_axis',(0.939338984774712,-0.342990191816636,0.));
#35203=DIRECTION('',(0.,0.,-1.));
#35204=DIRECTION('center_axis',(0.,0.,-1.));
#35205=DIRECTION('ref_axis',(0.939338984774712,-0.342990191816636,0.));
#35206=DIRECTION('',(0.,0.,-1.));
#35207=DIRECTION('center_axis',(0.,0.,-1.));
#35208=DIRECTION('ref_axis',(0.939338984774712,-0.342990191816636,0.));
#35209=DIRECTION('',(0.,0.,-1.));
#35210=DIRECTION('center_axis',(0.,0.,-1.));
#35211=DIRECTION('ref_axis',(0.939338984774712,-0.342990191816636,0.));
#35212=DIRECTION('',(0.,0.,-1.));
#35213=DIRECTION('center_axis',(0.,0.,-1.));
#35214=DIRECTION('ref_axis',(0.939338984774712,-0.342990191816636,0.));
#35215=DIRECTION('',(0.,0.,-1.));
#35216=DIRECTION('center_axis',(0.,0.,-1.));
#35217=DIRECTION('ref_axis',(0.939338984774712,-0.342990191816636,0.));
#35218=DIRECTION('',(0.,0.,-1.));
#35219=DIRECTION('center_axis',(0.,0.,-1.));
#35220=DIRECTION('ref_axis',(0.939338984774712,-0.342990191816636,0.));
#35221=DIRECTION('',(0.,0.,-1.));
#35222=DIRECTION('center_axis',(0.,0.,-1.));
#35223=DIRECTION('ref_axis',(0.939338984774712,-0.342990191816636,0.));
#35224=DIRECTION('',(0.,0.,-1.));
#35225=DIRECTION('center_axis',(0.,0.,-1.));
#35226=DIRECTION('ref_axis',(0.939338984774712,-0.342990191816636,0.));
#35227=DIRECTION('',(0.,0.,-1.));
#35228=DIRECTION('center_axis',(0.,0.,-1.));
#35229=DIRECTION('ref_axis',(0.939338984774712,-0.342990191816636,0.));
#35230=DIRECTION('',(0.,0.,-1.));
#35231=DIRECTION('center_axis',(0.,0.,-1.));
#35232=DIRECTION('ref_axis',(0.939338984774712,-0.342990191816636,0.));
#35233=DIRECTION('',(0.,0.,-1.));
#35234=DIRECTION('center_axis',(0.,0.,-1.));
#35235=DIRECTION('ref_axis',(0.939338988036949,-0.342990182882426,0.));
#35236=DIRECTION('',(0.,0.,-1.));
#35237=DIRECTION('center_axis',(0.,0.,1.));
#35238=DIRECTION('ref_axis',(1.,0.,0.));
#35239=DIRECTION('center_axis',(0.,0.,-1.));
#35240=DIRECTION('ref_axis',(0.939338988036949,-0.342990182882426,0.));
#35241=DIRECTION('',(0.,0.,-1.));
#35242=DIRECTION('center_axis',(0.,0.,-1.));
#35243=DIRECTION('ref_axis',(0.939338988036949,-0.342990182882426,0.));
#35244=DIRECTION('',(0.,0.,-1.));
#35245=DIRECTION('center_axis',(0.,0.,-1.));
#35246=DIRECTION('ref_axis',(0.939338988036949,-0.342990182882426,0.));
#35247=DIRECTION('',(0.,0.,-1.));
#35248=DIRECTION('center_axis',(0.,0.,-1.));
#35249=DIRECTION('ref_axis',(0.939338988036949,-0.342990182882426,0.));
#35250=DIRECTION('',(0.,0.,-1.));
#35251=DIRECTION('center_axis',(0.,0.,-1.));
#35252=DIRECTION('ref_axis',(0.939338988036949,-0.342990182882426,0.));
#35253=DIRECTION('',(0.,0.,-1.));
#35254=DIRECTION('center_axis',(0.,0.,-1.));
#35255=DIRECTION('ref_axis',(0.939338988036949,-0.342990182882426,0.));
#35256=DIRECTION('',(0.,0.,-1.));
#35257=DIRECTION('center_axis',(0.,0.,-1.));
#35258=DIRECTION('ref_axis',(0.939338988036949,-0.342990182882426,0.));
#35259=DIRECTION('',(0.,0.,-1.));
#35260=DIRECTION('center_axis',(0.,0.,-1.));
#35261=DIRECTION('ref_axis',(0.939338988036949,-0.342990182882426,0.));
#35262=DIRECTION('',(0.,0.,-1.));
#35263=DIRECTION('center_axis',(0.,0.,-1.));
#35264=DIRECTION('ref_axis',(0.939338988036949,-0.342990182882426,0.));
#35265=DIRECTION('',(0.,0.,-1.));
#35266=DIRECTION('center_axis',(0.,0.,-1.));
#35267=DIRECTION('ref_axis',(0.939338988036949,-0.342990182882426,0.));
#35268=DIRECTION('',(0.,0.,-1.));
#35269=DIRECTION('center_axis',(0.,0.,-1.));
#35270=DIRECTION('ref_axis',(0.939338988036949,-0.342990182882426,0.));
#35271=DIRECTION('',(0.,0.,-1.));
#35272=DIRECTION('center_axis',(0.,0.,-1.));
#35273=DIRECTION('ref_axis',(0.939338988036949,-0.342990182882426,0.));
#35274=DIRECTION('',(0.,0.,-1.));
#35275=DIRECTION('center_axis',(0.,0.,-1.));
#35276=DIRECTION('ref_axis',(0.939338988036949,-0.342990182882426,0.));
#35277=DIRECTION('',(0.,0.,-1.));
#35278=DIRECTION('center_axis',(0.,0.,-1.));
#35279=DIRECTION('ref_axis',(0.939338988036949,-0.342990182882426,0.));
#35280=DIRECTION('',(0.,0.,-1.));
#35281=DIRECTION('center_axis',(0.,0.,-1.));
#35282=DIRECTION('ref_axis',(0.939338988036949,-0.342990182882426,0.));
#35283=DIRECTION('',(0.,0.,-1.));
#35284=DIRECTION('center_axis',(0.,0.,-1.));
#35285=DIRECTION('ref_axis',(0.939338988036949,-0.342990182882426,0.));
#35286=DIRECTION('',(0.,0.,-1.));
#35287=DIRECTION('center_axis',(0.,0.,-1.));
#35288=DIRECTION('ref_axis',(0.939338988036949,-0.342990182882426,0.));
#35289=DIRECTION('',(0.,0.,-1.));
#35290=DIRECTION('center_axis',(0.,0.,-1.));
#35291=DIRECTION('ref_axis',(0.939338988036949,-0.342990182882426,0.));
#35292=DIRECTION('',(0.,0.,-1.));
#35293=DIRECTION('center_axis',(0.,0.,-1.));
#35294=DIRECTION('ref_axis',(0.939338988036949,-0.342990182882426,0.));
#35295=DIRECTION('',(0.,0.,-1.));
#35296=DIRECTION('center_axis',(0.,0.,-1.));
#35297=DIRECTION('ref_axis',(0.939338988036949,-0.342990182882426,0.));
#35298=DIRECTION('',(0.,0.,-1.));
#35299=DIRECTION('center_axis',(0.,0.,-1.));
#35300=DIRECTION('ref_axis',(0.939338988036949,-0.342990182882426,0.));
#35301=DIRECTION('',(0.,0.,-1.));
#35302=DIRECTION('center_axis',(0.,0.,-1.));
#35303=DIRECTION('ref_axis',(0.939338988036949,-0.342990182882426,0.));
#35304=DIRECTION('',(0.,0.,-1.));
#35305=DIRECTION('center_axis',(0.,0.,-1.));
#35306=DIRECTION('ref_axis',(0.939338988036949,-0.342990182882426,0.));
#35307=DIRECTION('',(0.,0.,-1.));
#35308=DIRECTION('center_axis',(0.,0.,-1.));
#35309=DIRECTION('ref_axis',(0.939338988036949,-0.342990182882426,0.));
#35310=DIRECTION('',(0.,0.,-1.));
#35311=DIRECTION('center_axis',(0.,0.,-1.));
#35312=DIRECTION('ref_axis',(0.939338988036949,-0.342990182882426,0.));
#35313=DIRECTION('',(0.,0.,-1.));
#35314=DIRECTION('center_axis',(0.,0.,-1.));
#35315=DIRECTION('ref_axis',(0.939338988036949,-0.342990182882426,0.));
#35316=DIRECTION('',(0.,0.,-1.));
#35317=DIRECTION('center_axis',(0.,0.,-1.));
#35318=DIRECTION('ref_axis',(0.939338973287599,-0.342990223276114,0.));
#35319=DIRECTION('',(0.,0.,-1.));
#35320=DIRECTION('center_axis',(0.,0.,1.));
#35321=DIRECTION('ref_axis',(1.,0.,0.));
#35322=DIRECTION('center_axis',(0.,0.,-1.));
#35323=DIRECTION('ref_axis',(0.939338973287599,-0.342990223276114,0.));
#35324=DIRECTION('',(0.,0.,-1.));
#35325=DIRECTION('center_axis',(0.,0.,-1.));
#35326=DIRECTION('ref_axis',(0.939338973287599,-0.342990223276114,0.));
#35327=DIRECTION('',(0.,0.,-1.));
#35328=DIRECTION('center_axis',(0.,0.,-1.));
#35329=DIRECTION('ref_axis',(0.939338973287599,-0.342990223276114,0.));
#35330=DIRECTION('',(0.,0.,-1.));
#35331=DIRECTION('center_axis',(0.,0.,-1.));
#35332=DIRECTION('ref_axis',(0.939338973287599,-0.342990223276114,0.));
#35333=DIRECTION('',(0.,0.,-1.));
#35334=DIRECTION('center_axis',(0.,0.,-1.));
#35335=DIRECTION('ref_axis',(0.939338973287599,-0.342990223276114,0.));
#35336=DIRECTION('',(0.,0.,-1.));
#35337=DIRECTION('center_axis',(0.,0.,-1.));
#35338=DIRECTION('ref_axis',(0.939338973287599,-0.342990223276114,0.));
#35339=DIRECTION('',(0.,0.,-1.));
#35340=DIRECTION('center_axis',(0.,0.,-1.));
#35341=DIRECTION('ref_axis',(0.939338973287599,-0.342990223276114,0.));
#35342=DIRECTION('',(0.,0.,-1.));
#35343=DIRECTION('center_axis',(0.,0.,-1.));
#35344=DIRECTION('ref_axis',(0.939338973287599,-0.342990223276114,0.));
#35345=DIRECTION('',(0.,0.,-1.));
#35346=DIRECTION('center_axis',(0.,0.,-1.));
#35347=DIRECTION('ref_axis',(0.939338973287599,-0.342990223276114,0.));
#35348=DIRECTION('',(0.,0.,-1.));
#35349=DIRECTION('center_axis',(0.,0.,-1.));
#35350=DIRECTION('ref_axis',(0.939338973287599,-0.342990223276114,0.));
#35351=DIRECTION('',(0.,0.,-1.));
#35352=DIRECTION('center_axis',(0.,0.,-1.));
#35353=DIRECTION('ref_axis',(0.939338973287599,-0.342990223276114,0.));
#35354=DIRECTION('',(0.,0.,-1.));
#35355=DIRECTION('center_axis',(0.,0.,-1.));
#35356=DIRECTION('ref_axis',(0.939338973287599,-0.342990223276114,0.));
#35357=DIRECTION('',(0.,0.,-1.));
#35358=DIRECTION('center_axis',(0.,0.,-1.));
#35359=DIRECTION('ref_axis',(0.939338973287599,-0.342990223276114,0.));
#35360=DIRECTION('',(0.,0.,-1.));
#35361=DIRECTION('center_axis',(0.,0.,-1.));
#35362=DIRECTION('ref_axis',(0.939338973287599,-0.342990223276114,0.));
#35363=DIRECTION('',(0.,0.,-1.));
#35364=DIRECTION('center_axis',(0.,0.,-1.));
#35365=DIRECTION('ref_axis',(0.939338973287599,-0.342990223276114,0.));
#35366=DIRECTION('',(0.,0.,-1.));
#35367=DIRECTION('center_axis',(0.,0.,-1.));
#35368=DIRECTION('ref_axis',(0.939338973287599,-0.342990223276114,0.));
#35369=DIRECTION('',(0.,0.,-1.));
#35370=DIRECTION('center_axis',(0.,0.,-1.));
#35371=DIRECTION('ref_axis',(0.939338973287599,-0.342990223276114,0.));
#35372=DIRECTION('',(0.,0.,-1.));
#35373=DIRECTION('center_axis',(0.,0.,-1.));
#35374=DIRECTION('ref_axis',(0.939338973287599,-0.342990223276114,0.));
#35375=DIRECTION('',(0.,0.,-1.));
#35376=DIRECTION('center_axis',(0.,0.,-1.));
#35377=DIRECTION('ref_axis',(0.939338973287599,-0.342990223276114,0.));
#35378=DIRECTION('',(0.,0.,-1.));
#35379=DIRECTION('center_axis',(0.,0.,-1.));
#35380=DIRECTION('ref_axis',(0.939338973287599,-0.342990223276114,0.));
#35381=DIRECTION('',(0.,0.,-1.));
#35382=DIRECTION('center_axis',(0.,0.,-1.));
#35383=DIRECTION('ref_axis',(0.939338973287599,-0.342990223276114,0.));
#35384=DIRECTION('',(0.,0.,-1.));
#35385=DIRECTION('center_axis',(0.,0.,-1.));
#35386=DIRECTION('ref_axis',(0.939338973287599,-0.342990223276114,0.));
#35387=DIRECTION('',(0.,0.,-1.));
#35388=DIRECTION('center_axis',(0.,0.,-1.));
#35389=DIRECTION('ref_axis',(0.939338973287599,-0.342990223276114,0.));
#35390=DIRECTION('',(0.,0.,-1.));
#35391=DIRECTION('center_axis',(0.,0.,-1.));
#35392=DIRECTION('ref_axis',(0.939338973287599,-0.342990223276114,0.));
#35393=DIRECTION('',(0.,0.,-1.));
#35394=DIRECTION('center_axis',(0.,0.,-1.));
#35395=DIRECTION('ref_axis',(0.939338973287599,-0.342990223276114,0.));
#35396=DIRECTION('',(0.,0.,-1.));
#35397=DIRECTION('center_axis',(0.,0.,-1.));
#35398=DIRECTION('ref_axis',(0.939338973287599,-0.342990223276114,0.));
#35399=DIRECTION('',(0.,0.,-1.));
#35400=DIRECTION('center_axis',(0.,0.,-1.));
#35401=DIRECTION('ref_axis',(0.939338973287599,-0.342990223276114,0.));
#35402=DIRECTION('center_axis',(0.,0.,1.));
#35403=DIRECTION('ref_axis',(1.,0.,0.));
#35404=DIRECTION('center_axis',(0.,0.,-1.));
#35405=DIRECTION('ref_axis',(0.939338988036949,-0.342990182882426,0.));
#35406=DIRECTION('center_axis',(0.,0.,1.));
#35407=DIRECTION('ref_axis',(1.,0.,0.));
#35408=DIRECTION('center_axis',(0.,0.,-1.));
#35409=DIRECTION('ref_axis',(0.939338984774712,-0.342990191816636,0.));
#35410=DIRECTION('center_axis',(0.,0.,1.));
#35411=DIRECTION('ref_axis',(1.,0.,0.));
#35412=DIRECTION('center_axis',(0.,0.,-1.));
#35413=DIRECTION('ref_axis',(0.939338957847042,-0.34299026556279,0.));
#35414=DIRECTION('center_axis',(0.,0.,1.));
#35415=DIRECTION('ref_axis',(1.,0.,0.));
#35416=DIRECTION('center_axis',(-1.,0.,0.));
#35417=DIRECTION('ref_axis',(0.,0.,-1.));
#35418=DIRECTION('center_axis',(-1.,0.,0.));
#35419=DIRECTION('ref_axis',(0.,0.,-1.));
#35420=DIRECTION('center_axis',(-1.,0.,0.));
#35421=DIRECTION('ref_axis',(0.,0.,-1.));
#35422=DIRECTION('center_axis',(1.,0.,0.));
#35423=DIRECTION('ref_axis',(0.,0.,-1.));
#35424=DIRECTION('center_axis',(0.,0.,-1.));
#35425=DIRECTION('ref_axis',(-0.609193695218696,0.793021463584555,0.));
#35426=DIRECTION('center_axis',(0.,0.,1.));
#35427=DIRECTION('ref_axis',(1.,7.89299181569448E-14,0.));
#35428=DIRECTION('center_axis',(0.,0.,-1.));
#35429=DIRECTION('ref_axis',(-0.609193651103488,0.793021497473556,0.));
#35430=DIRECTION('center_axis',(0.,0.,1.));
#35431=DIRECTION('ref_axis',(1.,7.80625564189562E-14,0.));
#35432=DIRECTION('center_axis',(0.,0.,-1.));
#35433=DIRECTION('ref_axis',(-0.609193645039877,0.793021502131581,0.));
#35434=DIRECTION('center_axis',(0.,0.,1.));
#35435=DIRECTION('ref_axis',(1.,8.15320033709099E-14,0.));
#35436=DIRECTION('center_axis',(0.,0.,-1.));
#35437=DIRECTION('ref_axis',(-0.609193659724225,0.793021490851165,0.));
#35438=DIRECTION('center_axis',(0.,0.,1.));
#35439=DIRECTION('ref_axis',(1.,8.06646416329218E-14,0.));
#35440=DIRECTION('center_axis',(1.,0.,0.));
#35441=DIRECTION('ref_axis',(0.,-0.878663231892279,-0.477442064465015));
#35442=DIRECTION('center_axis',(-1.,0.,0.));
#35443=DIRECTION('ref_axis',(0.,-1.74186785585433E-15,-1.));
#35444=DIRECTION('center_axis',(-1.,0.,0.));
#35445=DIRECTION('ref_axis',(0.,0.878663232865503,-0.477442062673936));
#35446=DIRECTION('center_axis',(1.,0.,0.));
#35447=DIRECTION('ref_axis',(0.,-1.74186785585433E-15,-1.));
#35448=DIRECTION('center_axis',(0.,0.,1.));
#35449=DIRECTION('ref_axis',(1.,0.,0.));
#35450=DIRECTION('center_axis',(0.,0.,1.));
#35451=DIRECTION('ref_axis',(1.,0.,0.));
#35452=DIRECTION('',(0.,0.,1.));
#35453=DIRECTION('center_axis',(0.,0.,1.));
#35454=DIRECTION('ref_axis',(1.,0.,0.));
#35455=DIRECTION('center_axis',(0.,0.,-1.));
#35456=DIRECTION('ref_axis',(-1.,0.,0.));
#35457=DIRECTION('center_axis',(0.,0.,1.));
#35458=DIRECTION('ref_axis',(1.,0.,0.));
#35459=DIRECTION('center_axis',(0.,0.,1.));
#35460=DIRECTION('ref_axis',(1.,0.,0.));
#35461=DIRECTION('',(0.,0.,-1.));
#35462=DIRECTION('center_axis',(0.,0.,1.));
#35463=DIRECTION('ref_axis',(1.,0.,0.));
#35464=DIRECTION('',(0.,0.,1.));
#35465=DIRECTION('center_axis',(0.,0.,-1.));
#35466=DIRECTION('ref_axis',(-1.,0.,0.));
#35467=DIRECTION('',(0.,-1.,0.));
#35468=DIRECTION('center_axis',(0.,0.,1.));
#35469=DIRECTION('ref_axis',(-0.374029024133323,0.927416998499529,0.));
#35470=DIRECTION('',(0.,-1.,0.));
#35471=DIRECTION('',(-1.,0.,0.));
#35472=DIRECTION('center_axis',(0.,0.,1.));
#35473=DIRECTION('ref_axis',(1.,0.,0.));
#35474=DIRECTION('center_axis',(0.,0.,1.));
#35475=DIRECTION('ref_axis',(1.,0.,0.));
#35476=DIRECTION('',(0.,0.,1.));
#35477=DIRECTION('center_axis',(0.,0.,1.));
#35478=DIRECTION('ref_axis',(1.,0.,0.));
#35479=DIRECTION('center_axis',(0.,0.,-1.));
#35480=DIRECTION('ref_axis',(-1.,0.,0.));
#35481=DIRECTION('center_axis',(0.,0.,1.));
#35482=DIRECTION('ref_axis',(-0.873226700271574,-0.487314200421882,0.));
#35483=DIRECTION('center_axis',(0.,0.,1.));
#35484=DIRECTION('ref_axis',(1.,0.,0.));
#35485=DIRECTION('',(0.,0.,-1.));
#35486=DIRECTION('center_axis',(0.,0.,1.));
#35487=DIRECTION('ref_axis',(1.,0.,0.));
#35488=DIRECTION('',(0.,0.,1.));
#35489=DIRECTION('center_axis',(0.,0.,-1.));
#35490=DIRECTION('ref_axis',(-1.,0.,0.));
#35491=DIRECTION('',(0.,1.,0.));
#35492=DIRECTION('center_axis',(0.,0.,1.));
#35493=DIRECTION('ref_axis',(0.914708142118334,0.404115100859181,0.));
#35494=DIRECTION('',(0.,1.,0.));
#35495=DIRECTION('',(-1.,0.,0.));
#35496=DIRECTION('center_axis',(0.,0.,1.));
#35497=DIRECTION('ref_axis',(1.,0.,0.));
#35498=DIRECTION('center_axis',(0.,0.,1.));
#35499=DIRECTION('ref_axis',(1.,0.,0.));
#35500=DIRECTION('',(0.,0.,1.));
#35501=DIRECTION('center_axis',(0.,0.,1.));
#35502=DIRECTION('ref_axis',(1.,0.,0.));
#35503=DIRECTION('center_axis',(0.,0.,-1.));
#35504=DIRECTION('ref_axis',(-1.,0.,0.));
#35505=DIRECTION('center_axis',(1.,0.,0.));
#35506=DIRECTION('ref_axis',(0.,1.,0.));
#35507=DIRECTION('',(0.,0.,1.));
#35508=DIRECTION('',(0.,1.,0.));
#35509=DIRECTION('',(0.,0.,1.));
#35510=DIRECTION('center_axis',(-1.,0.,0.));
#35511=DIRECTION('ref_axis',(0.,-1.,0.));
#35512=DIRECTION('',(0.,0.,1.));
#35513=DIRECTION('',(0.,1.,0.));
#35514=DIRECTION('',(0.,0.,1.));
#35515=DIRECTION('',(0.,-1.,0.));
#35516=DIRECTION('center_axis',(0.,-1.,0.));
#35517=DIRECTION('ref_axis',(1.,0.,0.));
#35518=DIRECTION('',(-1.,0.,0.));
#35519=DIRECTION('',(0.,0.,1.));
#35520=DIRECTION('',(1.,0.,0.));
#35521=DIRECTION('center_axis',(0.,0.,1.));
#35522=DIRECTION('ref_axis',(1.,0.,0.));
#35523=DIRECTION('center_axis',(0.,0.,1.));
#35524=DIRECTION('ref_axis',(0.,1.,0.));
#35525=DIRECTION('',(-1.,0.,0.));
#35526=DIRECTION('center_axis',(0.,0.,-1.));
#35527=DIRECTION('ref_axis',(0.,-1.,0.));
#35528=DIRECTION('',(0.,-1.,0.));
#35529=DIRECTION('center_axis',(0.,0.,-1.));
#35530=DIRECTION('ref_axis',(1.,0.,0.));
#35531=DIRECTION('',(0.987070639057186,0.160285849379284,0.));
#35532=DIRECTION('center_axis',(0.,0.,-1.));
#35533=DIRECTION('ref_axis',(0.,1.,0.));
#35534=DIRECTION('',(0.,1.,0.));
#35535=DIRECTION('',(-1.,0.,0.));
#35536=DIRECTION('',(0.,1.,0.));
#35537=DIRECTION('',(1.,0.,0.));
#35538=DIRECTION('',(0.,1.,0.));
#35539=DIRECTION('center_axis',(0.,0.,-1.));
#35540=DIRECTION('ref_axis',(-1.,0.,0.));
#35541=DIRECTION('',(-1.,3.69197497485193E-16,0.));
#35542=DIRECTION('center_axis',(0.,0.,-1.));
#35543=DIRECTION('ref_axis',(0.,-1.,0.));
#35544=DIRECTION('',(0.,-1.,0.));
#35545=DIRECTION('',(1.,0.,0.));
#35546=DIRECTION('',(0.,-1.,0.));
#35547=DIRECTION('',(-1.,0.,0.));
#35548=DIRECTION('',(0.,-1.,0.));
#35549=DIRECTION('center_axis',(0.,0.,-1.));
#35550=DIRECTION('ref_axis',(1.,4.44089209850062E-16,0.));
#35551=DIRECTION('',(0.987070639057186,-0.160285849379284,0.));
#35552=DIRECTION('center_axis',(0.,0.,-1.));
#35553=DIRECTION('ref_axis',(0.,1.,0.));
#35554=DIRECTION('',(0.,1.,0.));
#35555=DIRECTION('center_axis',(0.,0.,-1.));
#35556=DIRECTION('ref_axis',(-1.,0.,0.));
#35557=DIRECTION('',(-1.,0.,0.));
#35558=DIRECTION('center_axis',(0.,0.,1.));
#35559=DIRECTION('ref_axis',(1.,0.,0.));
#35560=DIRECTION('',(0.,1.,0.));
#35561=DIRECTION('center_axis',(0.,0.,1.));
#35562=DIRECTION('ref_axis',(1.,0.,0.));
#35563=DIRECTION('center_axis',(0.,0.,1.));
#35564=DIRECTION('ref_axis',(1.,0.,0.));
#35565=DIRECTION('center_axis',(0.,0.,1.));
#35566=DIRECTION('ref_axis',(0.,1.,0.));
#35567=DIRECTION('',(0.,-1.,0.));
#35568=DIRECTION('',(-1.,0.,0.));
#35569=DIRECTION('',(0.,1.,0.));
#35570=DIRECTION('',(-1.,0.,0.));
#35571=DIRECTION('center_axis',(0.,1.,0.));
#35572=DIRECTION('ref_axis',(0.,0.,-1.));
#35573=DIRECTION('',(0.,0.,1.));
#35574=DIRECTION('',(-1.,0.,0.));
#35575=DIRECTION('',(0.,0.,-1.));
#35576=DIRECTION('center_axis',(0.,0.,1.));
#35577=DIRECTION('ref_axis',(0.,1.,0.));
#35578=DIRECTION('',(0.,-1.,0.));
#35579=DIRECTION('',(-1.,0.,0.));
#35580=DIRECTION('',(0.,1.,0.));
#35581=DIRECTION('center_axis',(0.,0.894427190999916,-0.447213595499957));
#35582=DIRECTION('ref_axis',(0.,-0.447213595499957,-0.894427190999916));
#35583=DIRECTION('',(0.,0.447213595499957,0.894427190999916));
#35584=DIRECTION('',(-1.,0.,0.));
#35585=DIRECTION('',(0.,-0.447213595499957,-0.894427190999916));
#35586=DIRECTION('center_axis',(0.,-0.894427190999916,-0.447213595499957));
#35587=DIRECTION('ref_axis',(0.,-0.447213595499957,0.894427190999916));
#35588=DIRECTION('',(0.,0.447213595499957,-0.894427190999916));
#35589=DIRECTION('',(-1.,0.,0.));
#35590=DIRECTION('',(0.,-0.447213595499957,0.894427190999916));
#35591=DIRECTION('center_axis',(0.,0.,1.));
#35592=DIRECTION('ref_axis',(0.,1.,0.));
#35593=DIRECTION('',(0.,-1.,0.));
#35594=DIRECTION('',(-1.,0.,0.));
#35595=DIRECTION('',(0.,1.,0.));
#35596=DIRECTION('center_axis',(0.,-1.,0.));
#35597=DIRECTION('ref_axis',(0.,0.,1.));
#35598=DIRECTION('',(0.,0.,-1.));
#35599=DIRECTION('',(0.,0.,1.));
#35600=DIRECTION('center_axis',(-1.,0.,0.));
#35601=DIRECTION('ref_axis',(0.,0.,-1.));
#35602=DIRECTION('center_axis',(1.,0.,0.));
#35603=DIRECTION('ref_axis',(0.,0.,-1.));
#35604=DIRECTION('',(-1.,0.,0.));
#35605=DIRECTION('center_axis',(-1.,0.,0.));
#35606=DIRECTION('ref_axis',(0.,0.,-1.));
#35607=DIRECTION('center_axis',(1.,0.,0.));
#35608=DIRECTION('ref_axis',(0.,0.,-1.));
#35609=DIRECTION('center_axis',(-1.,0.,0.));
#35610=DIRECTION('ref_axis',(0.,-0.912870929175277,-0.408248290463863));
#35611=DIRECTION('center_axis',(1.,0.,0.));
#35612=DIRECTION('ref_axis',(0.,0.,-1.));
#35613=DIRECTION('',(-1.,0.,0.));
#35614=DIRECTION('center_axis',(-1.,0.,0.));
#35615=DIRECTION('ref_axis',(0.,0.,-1.));
#35616=DIRECTION('',(-1.,0.,0.));
#35617=DIRECTION('center_axis',(0.,0.,-1.));
#35618=DIRECTION('ref_axis',(0.,-1.,0.));
#35619=DIRECTION('',(0.,1.,0.));
#35620=DIRECTION('',(-1.,0.,0.));
#35621=DIRECTION('',(0.,-1.,0.));
#35622=DIRECTION('center_axis',(-1.,0.,0.));
#35623=DIRECTION('ref_axis',(0.,0.912870929175277,-0.408248290463863));
#35624=DIRECTION('center_axis',(1.,0.,0.));
#35625=DIRECTION('ref_axis',(0.,0.,-1.));
#35626=DIRECTION('',(-1.,0.,0.));
#35627=DIRECTION('center_axis',(-1.,0.,0.));
#35628=DIRECTION('ref_axis',(0.,0.,-1.));
#35629=DIRECTION('center_axis',(0.,1.,0.));
#35630=DIRECTION('ref_axis',(0.,0.,-1.));
#35631=DIRECTION('',(0.,0.,1.));
#35632=DIRECTION('',(0.,0.,-1.));
#35633=DIRECTION('center_axis',(0.,-1.,0.));
#35634=DIRECTION('ref_axis',(0.,0.,1.));
#35635=DIRECTION('',(0.,0.,-1.));
#35636=DIRECTION('',(0.,0.,1.));
#35637=DIRECTION('center_axis',(1.,0.,0.));
#35638=DIRECTION('ref_axis',(0.,0.,-1.));
#35639=DIRECTION('center_axis',(-1.,0.,0.));
#35640=DIRECTION('ref_axis',(0.,0.,-1.));
#35641=DIRECTION('center_axis',(-1.,0.,0.));
#35642=DIRECTION('ref_axis',(0.,0.,-1.));
#35643=DIRECTION('center_axis',(0.,-1.,0.));
#35644=DIRECTION('ref_axis',(0.,0.,1.));
#35645=DIRECTION('',(0.,0.,-1.));
#35646=DIRECTION('',(-1.,0.,0.));
#35647=DIRECTION('',(0.,0.,1.));
#35648=DIRECTION('',(-1.,0.,0.));
#35649=DIRECTION('center_axis',(0.,0.,-1.));
#35650=DIRECTION('ref_axis',(0.,-1.,0.));
#35651=DIRECTION('',(0.,1.,0.));
#35652=DIRECTION('',(-1.,0.,0.));
#35653=DIRECTION('',(0.,-1.,0.));
#35654=DIRECTION('center_axis',(0.,-0.894427190999916,0.447213595499958));
#35655=DIRECTION('ref_axis',(0.,0.447213595499958,0.894427190999916));
#35656=DIRECTION('',(0.,-0.447213595499958,-0.894427190999916));
#35657=DIRECTION('',(-1.,0.,0.));
#35658=DIRECTION('',(0.,0.447213595499958,0.894427190999916));
#35659=DIRECTION('center_axis',(0.,0.894427190999916,0.447213595499958));
#35660=DIRECTION('ref_axis',(0.,0.447213595499958,-0.894427190999916));
#35661=DIRECTION('',(0.,-0.447213595499958,0.894427190999916));
#35662=DIRECTION('',(-1.,0.,0.));
#35663=DIRECTION('',(0.,0.447213595499958,-0.894427190999916));
#35664=DIRECTION('center_axis',(0.,0.,-1.));
#35665=DIRECTION('ref_axis',(0.,-1.,0.));
#35666=DIRECTION('',(0.,1.,0.));
#35667=DIRECTION('',(-1.,0.,0.));
#35668=DIRECTION('',(0.,-1.,0.));
#35669=DIRECTION('center_axis',(0.,1.,0.));
#35670=DIRECTION('ref_axis',(0.,0.,-1.));
#35671=DIRECTION('',(0.,0.,1.));
#35672=DIRECTION('',(-1.,0.,0.));
#35673=DIRECTION('',(0.,0.,-1.));
#35674=DIRECTION('center_axis',(0.,0.,-1.));
#35675=DIRECTION('ref_axis',(0.,-1.,0.));
#35676=DIRECTION('',(0.,1.,0.));
#35677=DIRECTION('',(0.,-1.,0.));
#35678=DIRECTION('center_axis',(-1.,0.,0.));
#35679=DIRECTION('ref_axis',(0.,0.,-1.));
#35680=DIRECTION('center_axis',(1.,0.,0.));
#35681=DIRECTION('ref_axis',(0.,0.,-1.));
#35682=DIRECTION('',(-1.,0.,0.));
#35683=DIRECTION('center_axis',(-1.,0.,0.));
#35684=DIRECTION('ref_axis',(0.,0.,-1.));
#35685=DIRECTION('center_axis',(1.,0.,0.));
#35686=DIRECTION('ref_axis',(0.,0.,-1.));
#35687=DIRECTION('center_axis',(-1.,0.,0.));
#35688=DIRECTION('ref_axis',(0.,-1.,0.));
#35689=DIRECTION('center_axis',(-1.,0.,0.));
#35690=DIRECTION('ref_axis',(0.,-1.,0.));
#35691=DIRECTION('center_axis',(-1.,0.,0.));
#35692=DIRECTION('ref_axis',(0.,0.,-1.));
#35693=DIRECTION('',(-1.,0.,0.));
#35694=DIRECTION('center_axis',(-1.,0.,0.));
#35695=DIRECTION('ref_axis',(0.,0.,-1.));
#35696=DIRECTION('center_axis',(1.,0.,0.));
#35697=DIRECTION('ref_axis',(0.,0.,-1.));
#35698=DIRECTION('center_axis',(1.,0.,0.));
#35699=DIRECTION('ref_axis',(0.,0.,-1.));
#35700=DIRECTION('center_axis',(-1.,0.,0.));
#35701=DIRECTION('ref_axis',(0.,0.,-1.));
#35702=DIRECTION('',(-1.,0.,0.));
#35703=DIRECTION('center_axis',(-1.,0.,0.));
#35704=DIRECTION('ref_axis',(0.,0.,-1.));
#35705=DIRECTION('center_axis',(1.,0.,0.));
#35706=DIRECTION('ref_axis',(0.,0.,-1.));
#35707=DIRECTION('center_axis',(-1.,0.,0.));
#35708=DIRECTION('ref_axis',(0.,-0.912870929175277,-0.408248290463863));
#35709=DIRECTION('center_axis',(-1.,0.,0.));
#35710=DIRECTION('ref_axis',(0.,0.,-1.));
#35711=DIRECTION('',(1.,0.,0.));
#35712=DIRECTION('center_axis',(-1.,0.,0.));
#35713=DIRECTION('ref_axis',(0.,0.,-1.));
#35714=DIRECTION('',(1.,0.,0.));
#35715=DIRECTION('center_axis',(0.,0.,1.));
#35716=DIRECTION('ref_axis',(0.,-1.,0.));
#35717=DIRECTION('',(0.,-1.,0.));
#35718=DIRECTION('',(0.,-1.,0.));
#35719=DIRECTION('',(1.,0.,0.));
#35720=DIRECTION('center_axis',(-1.,0.,0.));
#35721=DIRECTION('ref_axis',(0.,0.912870929175277,-0.408248290463863));
#35722=DIRECTION('center_axis',(-1.,0.,0.));
#35723=DIRECTION('ref_axis',(0.,0.,-1.));
#35724=DIRECTION('center_axis',(-1.,0.,0.));
#35725=DIRECTION('ref_axis',(0.,0.,-1.));
#35726=DIRECTION('',(1.,0.,0.));
#35727=DIRECTION('center_axis',(0.,-1.,0.));
#35728=DIRECTION('ref_axis',(0.,0.,-1.));
#35729=DIRECTION('',(0.,0.,-1.));
#35730=DIRECTION('',(0.,0.,-1.));
#35731=DIRECTION('center_axis',(0.,1.,0.));
#35732=DIRECTION('ref_axis',(0.,0.,1.));
#35733=DIRECTION('',(0.,0.,1.));
#35734=DIRECTION('',(0.,0.,1.));
#35735=DIRECTION('center_axis',(1.,0.,0.));
#35736=DIRECTION('ref_axis',(0.,0.,-1.));
#35737=DIRECTION('center_axis',(1.,0.,0.));
#35738=DIRECTION('ref_axis',(0.,0.,-1.));
#35739=DIRECTION('center_axis',(1.,0.,0.));
#35740=DIRECTION('ref_axis',(0.,0.,-1.));
#35741=DIRECTION('center_axis',(0.,1.,0.));
#35742=DIRECTION('ref_axis',(0.,0.,1.));
#35743=DIRECTION('',(0.,0.,1.));
#35744=DIRECTION('',(1.,0.,0.));
#35745=DIRECTION('',(0.,0.,1.));
#35746=DIRECTION('',(1.,0.,0.));
#35747=DIRECTION('center_axis',(0.,0.,1.));
#35748=DIRECTION('ref_axis',(0.,-1.,0.));
#35749=DIRECTION('',(0.,-1.,0.));
#35750=DIRECTION('',(0.,-1.,0.));
#35751=DIRECTION('',(1.,0.,0.));
#35752=DIRECTION('center_axis',(0.,0.894427190999916,-0.447213595499958));
#35753=DIRECTION('ref_axis',(0.,0.447213595499958,0.894427190999916));
#35754=DIRECTION('',(0.,0.447213595499958,0.894427190999916));
#35755=DIRECTION('',(0.,0.447213595499958,0.894427190999916));
#35756=DIRECTION('',(1.,0.,0.));
#35757=DIRECTION('center_axis',(0.,-0.894427190999916,-0.447213595499958));
#35758=DIRECTION('ref_axis',(0.,0.447213595499958,-0.894427190999916));
#35759=DIRECTION('',(0.,0.447213595499958,-0.894427190999916));
#35760=DIRECTION('',(0.,0.447213595499958,-0.894427190999916));
#35761=DIRECTION('',(1.,0.,0.));
#35762=DIRECTION('center_axis',(0.,0.,1.));
#35763=DIRECTION('ref_axis',(0.,-1.,0.));
#35764=DIRECTION('',(0.,-1.,0.));
#35765=DIRECTION('',(0.,-1.,0.));
#35766=DIRECTION('',(1.,0.,0.));
#35767=DIRECTION('center_axis',(0.,-1.,0.));
#35768=DIRECTION('ref_axis',(0.,0.,-1.));
#35769=DIRECTION('',(0.,0.,-1.));
#35770=DIRECTION('',(0.,0.,-1.));
#35771=DIRECTION('',(1.,0.,0.));
#35772=DIRECTION('center_axis',(0.,0.,1.));
#35773=DIRECTION('ref_axis',(0.,-1.,0.));
#35774=DIRECTION('',(0.,-1.,0.));
#35775=DIRECTION('',(0.,-1.,0.));
#35776=DIRECTION('center_axis',(-1.,0.,0.));
#35777=DIRECTION('ref_axis',(0.,0.,-1.));
#35778=DIRECTION('center_axis',(-1.,0.,0.));
#35779=DIRECTION('ref_axis',(0.,0.,-1.));
#35780=DIRECTION('',(-1.,0.,0.));
#35781=DIRECTION('center_axis',(-1.,0.,0.));
#35782=DIRECTION('ref_axis',(0.,0.,-1.));
#35783=DIRECTION('center_axis',(1.,0.,0.));
#35784=DIRECTION('ref_axis',(0.,0.,-1.));
#35785=DIRECTION('center_axis',(0.,0.,-1.));
#35786=DIRECTION('ref_axis',(0.,1.,0.));
#35787=DIRECTION('',(0.,1.,0.));
#35788=DIRECTION('',(1.,0.,0.));
#35789=DIRECTION('',(0.,1.,0.));
#35790=DIRECTION('',(1.,0.,0.));
#35791=DIRECTION('center_axis',(0.,-1.,0.));
#35792=DIRECTION('ref_axis',(0.,0.,-1.));
#35793=DIRECTION('',(0.,0.,-1.));
#35794=DIRECTION('',(0.,0.,-1.));
#35795=DIRECTION('',(1.,0.,0.));
#35796=DIRECTION('center_axis',(0.,0.,-1.));
#35797=DIRECTION('ref_axis',(0.,1.,0.));
#35798=DIRECTION('',(0.,1.,0.));
#35799=DIRECTION('',(0.,1.,0.));
#35800=DIRECTION('',(1.,0.,0.));
#35801=DIRECTION('center_axis',(0.,-0.894427190999916,0.447213595499957));
#35802=DIRECTION('ref_axis',(0.,-0.447213595499957,-0.894427190999916));
#35803=DIRECTION('',(0.,-0.447213595499957,-0.894427190999916));
#35804=DIRECTION('',(0.,-0.447213595499957,-0.894427190999916));
#35805=DIRECTION('',(1.,0.,0.));
#35806=DIRECTION('center_axis',(0.,0.894427190999916,0.447213595499957));
#35807=DIRECTION('ref_axis',(0.,-0.447213595499957,0.894427190999916));
#35808=DIRECTION('',(0.,-0.447213595499957,0.894427190999916));
#35809=DIRECTION('',(0.,-0.447213595499957,0.894427190999916));
#35810=DIRECTION('',(1.,0.,0.));
#35811=DIRECTION('center_axis',(0.,0.,-1.));
#35812=DIRECTION('ref_axis',(0.,1.,0.));
#35813=DIRECTION('',(0.,1.,0.));
#35814=DIRECTION('',(0.,1.,0.));
#35815=DIRECTION('',(1.,0.,0.));
#35816=DIRECTION('center_axis',(0.,1.,0.));
#35817=DIRECTION('ref_axis',(0.,0.,1.));
#35818=DIRECTION('',(0.,0.,1.));
#35819=DIRECTION('',(0.,0.,1.));
#35820=DIRECTION('center_axis',(-1.,0.,0.));
#35821=DIRECTION('ref_axis',(0.,0.,-1.));
#35822=DIRECTION('center_axis',(-1.,0.,0.));
#35823=DIRECTION('ref_axis',(0.,0.,-1.));
#35824=DIRECTION('',(-1.,0.,0.));
#35825=DIRECTION('center_axis',(-1.,0.,0.));
#35826=DIRECTION('ref_axis',(0.,0.,-1.));
#35827=DIRECTION('center_axis',(1.,0.,0.));
#35828=DIRECTION('ref_axis',(0.,0.,-1.));
#35829=DIRECTION('center_axis',(1.,0.,0.));
#35830=DIRECTION('ref_axis',(0.,1.,0.));
#35831=DIRECTION('center_axis',(1.,0.,0.));
#35832=DIRECTION('ref_axis',(0.,1.,0.));
#35833=DIRECTION('center_axis',(1.,0.,0.));
#35834=DIRECTION('ref_axis',(0.,1.,0.));
#35835=DIRECTION('',(0.,0.,1.));
#35836=DIRECTION('',(0.,-1.,0.));
#35837=DIRECTION('',(0.,0.,1.));
#35838=DIRECTION('center_axis',(1.,0.,0.));
#35839=DIRECTION('ref_axis',(0.,0.,-1.));
#35840=DIRECTION('center_axis',(-1.,0.,0.));
#35841=DIRECTION('ref_axis',(0.,0.,-1.));
#35842=DIRECTION('center_axis',(-1.,0.,0.));
#35843=DIRECTION('ref_axis',(0.,0.,-1.));
#35844=DIRECTION('',(-1.,0.,0.));
#35845=DIRECTION('center_axis',(1.,0.,0.));
#35846=DIRECTION('ref_axis',(0.,0.,-1.));
#35847=DIRECTION('center_axis',(-1.,0.,0.));
#35848=DIRECTION('ref_axis',(0.,0.,-1.));
#35849=DIRECTION('center_axis',(-1.,0.,0.));
#35850=DIRECTION('ref_axis',(0.,0.,-1.));
#35851=DIRECTION('',(-1.,0.,0.));
#35852=DIRECTION('center_axis',(1.,0.,0.));
#35853=DIRECTION('ref_axis',(0.,0.,-1.));
#35854=DIRECTION('center_axis',(0.,0.,1.));
#35855=DIRECTION('ref_axis',(1.,0.,0.));
#35856=DIRECTION('center_axis',(0.,0.,1.));
#35857=DIRECTION('ref_axis',(1.,0.,0.));
#35858=DIRECTION('',(0.,0.,1.));
#35859=DIRECTION('center_axis',(0.,0.,-1.));
#35860=DIRECTION('ref_axis',(-1.,0.,0.));
#35861=DIRECTION('center_axis',(0.,0.,1.));
#35862=DIRECTION('ref_axis',(1.,0.,0.));
#35863=DIRECTION('center_axis',(0.,0.,1.));
#35864=DIRECTION('ref_axis',(1.,0.,0.));
#35865=DIRECTION('',(0.,0.,1.));
#35866=DIRECTION('center_axis',(0.,0.,-1.));
#35867=DIRECTION('ref_axis',(-1.,0.,0.));
#35868=DIRECTION('center_axis',(-1.,0.,0.));
#35869=DIRECTION('ref_axis',(0.,-1.,0.));
#35870=DIRECTION('',(0.,1.,0.));
#35871=DIRECTION('',(0.,0.,1.));
#35872=DIRECTION('center_axis',(0.,0.,-1.));
#35873=DIRECTION('ref_axis',(0.914708142118334,0.404115100859181,0.));
#35874=DIRECTION('center_axis',(0.,0.,1.));
#35875=DIRECTION('ref_axis',(0.914708142118334,0.404115100859181,0.));
#35876=DIRECTION('center_axis',(0.,0.,-1.));
#35877=DIRECTION('ref_axis',(0.,1.,0.));
#35878=DIRECTION('center_axis',(0.,0.,1.));
#35879=DIRECTION('ref_axis',(0.,1.,0.));
#35880=DIRECTION('',(0.,0.,1.));
#35881=DIRECTION('center_axis',(0.,1.,0.));
#35882=DIRECTION('ref_axis',(-1.,0.,0.));
#35883=DIRECTION('',(1.,0.,0.));
#35884=DIRECTION('',(0.,0.,1.));
#35885=DIRECTION('center_axis',(0.,0.,-1.));
#35886=DIRECTION('ref_axis',(0.,-1.,0.));
#35887=DIRECTION('center_axis',(0.,0.,1.));
#35888=DIRECTION('ref_axis',(0.,-1.,0.));
#35889=DIRECTION('',(0.,0.,1.));
#35890=DIRECTION('center_axis',(-1.,0.,0.));
#35891=DIRECTION('ref_axis',(0.,-1.,0.));
#35892=DIRECTION('',(0.,1.,0.));
#35893=DIRECTION('',(0.,0.,1.));
#35894=DIRECTION('center_axis',(0.,0.,-1.));
#35895=DIRECTION('ref_axis',(1.,0.,0.));
#35896=DIRECTION('center_axis',(0.,0.,1.));
#35897=DIRECTION('ref_axis',(1.,0.,0.));
#35898=DIRECTION('',(0.,0.,1.));
#35899=DIRECTION('center_axis',(0.160285849379284,-0.987070639057186,0.));
#35900=DIRECTION('ref_axis',(0.987070639057186,0.160285849379284,0.));
#35901=DIRECTION('',(-0.987070639057186,-0.160285849379284,0.));
#35902=DIRECTION('',(0.,0.,1.));
#35903=DIRECTION('center_axis',(0.,0.,-1.));
#35904=DIRECTION('ref_axis',(0.,1.,0.));
#35905=DIRECTION('center_axis',(0.,0.,1.));
#35906=DIRECTION('ref_axis',(0.,1.,0.));
#35907=DIRECTION('center_axis',(0.,0.,-1.));
#35908=DIRECTION('ref_axis',(-1.,0.,0.));
#35909=DIRECTION('center_axis',(0.,0.,1.));
#35910=DIRECTION('ref_axis',(-1.,0.,0.));
#35911=DIRECTION('',(0.,0.,1.));
#35912=DIRECTION('center_axis',(3.69197497485193E-16,1.,0.));
#35913=DIRECTION('ref_axis',(-1.,3.69197497485193E-16,0.));
#35914=DIRECTION('',(1.,-3.69197497485193E-16,0.));
#35915=DIRECTION('',(0.,0.,1.));
#35916=DIRECTION('center_axis',(0.,0.,-1.));
#35917=DIRECTION('ref_axis',(0.,-1.,0.));
#35918=DIRECTION('center_axis',(0.,0.,1.));
#35919=DIRECTION('ref_axis',(0.,-1.,0.));
#35920=DIRECTION('',(0.,0.,1.));
#35921=DIRECTION('center_axis',(-1.,0.,0.));
#35922=DIRECTION('ref_axis',(0.,-1.,0.));
#35923=DIRECTION('',(0.,-1.,0.));
#35924=DIRECTION('',(0.,0.,1.));
#35925=DIRECTION('center_axis',(0.,0.,-1.));
#35926=DIRECTION('ref_axis',(1.,4.44089209850062E-16,0.));
#35927=DIRECTION('center_axis',(0.,0.,1.));
#35928=DIRECTION('ref_axis',(1.,4.44089209850062E-16,0.));
#35929=DIRECTION('',(0.,0.,1.));
#35930=DIRECTION('center_axis',(-0.160285849379284,-0.987070639057186,0.));
#35931=DIRECTION('ref_axis',(0.987070639057186,-0.160285849379284,0.));
#35932=DIRECTION('',(0.987070639057186,-0.160285849379284,0.));
#35933=DIRECTION('',(0.,0.,1.));
#35934=DIRECTION('center_axis',(0.,0.,-1.));
#35935=DIRECTION('ref_axis',(0.,1.,0.));
#35936=DIRECTION('center_axis',(0.,0.,1.));
#35937=DIRECTION('ref_axis',(0.,1.,0.));
#35938=DIRECTION('',(0.,0.,1.));
#35939=DIRECTION('center_axis',(1.,0.,0.));
#35940=DIRECTION('ref_axis',(0.,1.,0.));
#35941=DIRECTION('',(0.,1.,0.));
#35942=DIRECTION('',(0.,0.,1.));
#35943=DIRECTION('center_axis',(0.,0.,-1.));
#35944=DIRECTION('ref_axis',(-1.,0.,0.));
#35945=DIRECTION('center_axis',(0.,0.,1.));
#35946=DIRECTION('ref_axis',(-1.,0.,0.));
#35947=DIRECTION('',(0.,0.,1.));
#35948=DIRECTION('center_axis',(0.,1.,0.));
#35949=DIRECTION('ref_axis',(-1.,0.,0.));
#35950=DIRECTION('',(-1.,0.,0.));
#35951=DIRECTION('',(0.,0.,1.));
#35952=DIRECTION('center_axis',(0.,0.,-1.));
#35953=DIRECTION('ref_axis',(1.,0.,0.));
#35954=DIRECTION('center_axis',(0.,0.,1.));
#35955=DIRECTION('ref_axis',(1.,0.,0.));
#35956=DIRECTION('',(0.,0.,1.));
#35957=DIRECTION('center_axis',(1.,0.,0.));
#35958=DIRECTION('ref_axis',(0.,1.,0.));
#35959=DIRECTION('',(0.,1.,0.));
#35960=DIRECTION('',(0.,0.,1.));
#35961=DIRECTION('center_axis',(0.,0.,-1.));
#35962=DIRECTION('ref_axis',(-0.374029024133323,0.927416998499529,0.));
#35963=DIRECTION('center_axis',(0.,0.,1.));
#35964=DIRECTION('ref_axis',(-0.374029024133323,0.927416998499529,0.));
#35965=DIRECTION('center_axis',(0.,0.,1.));
#35966=DIRECTION('ref_axis',(1.,0.,0.));
#128402=CARTESIAN_POINT('',(0.,0.,0.));
#128403=CARTESIAN_POINT('Origin',(-26.8463464956315,10.1295,7.));
#128404=CARTESIAN_POINT('',(-23.3525227612526,5.6491961756188,9.4344770775744));
#128405=CARTESIAN_POINT('',(-23.4778327537502,5.64975127298007,9.43417554508985));
#128406=CARTESIAN_POINT('',(-26.8463464956315,5.6491961756188,9.4344770775744));
#128407=CARTESIAN_POINT('',(-23.534,5.20511879703991,5.67702200776683));
#128408=CARTESIAN_POINT('Ctrl Pts',(-23.534,5.20511879703991,5.67702200776683));
#128409=CARTESIAN_POINT('Ctrl Pts',(-23.5270930683901,5.16684928138222,
5.81946858258322));
#128410=CARTESIAN_POINT('Ctrl Pts',(-23.5201861367802,5.13475838719278,
5.96360047114363));
#128411=CARTESIAN_POINT('Ctrl Pts',(-23.5132792051702,5.10897409853572,
6.10886551367019));
#128412=CARTESIAN_POINT('Ctrl Pts',(-23.5063724191029,5.08319035320424,
6.25412749517716));
#128413=CARTESIAN_POINT('Ctrl Pts',(-23.4994656330356,5.06371301191541,
6.40052225348957));
#128414=CARTESIAN_POINT('Ctrl Pts',(-23.4925588469683,5.05061883811789,
6.54748796316664));
#128415=CARTESIAN_POINT('Ctrl Pts',(-23.4856526672931,5.03752581394379,
6.69444076975994));
#128416=CARTESIAN_POINT('Ctrl Pts',(-23.4787464876178,5.03081486640317,
6.84196409317217));
#128417=CARTESIAN_POINT('Ctrl Pts',(-23.4718403079426,5.03051082838708,
6.98949153797162));
#128418=CARTESIAN_POINT('Ctrl Pts',(-23.4649324605092,5.03020671694952,
7.13705460884823));
#128419=CARTESIAN_POINT('Ctrl Pts',(-23.4580246130759,5.03631260848016,
7.28462146729368));
#128420=CARTESIAN_POINT('Ctrl Pts',(-23.4511167656425,5.04880119697881,
7.43162561668542));
#128421=CARTESIAN_POINT('Ctrl Pts',(-23.4457233772622,5.05855181882527,
7.54640094703871));
#128422=CARTESIAN_POINT('Ctrl Pts',(-23.4403299888818,5.07219222530018,
7.66083321109948));
#128423=CARTESIAN_POINT('Ctrl Pts',(-23.4349366005015,5.08968742686135,
7.77465490873909));
#128424=CARTESIAN_POINT('Ctrl Pts',(-23.4280025544932,5.11218025029517,
7.92099053905438));
#128425=CARTESIAN_POINT('Ctrl Pts',(-23.421068508485,5.14105472641507,8.06637105423135));
#128426=CARTESIAN_POINT('Ctrl Pts',(-23.4141344624767,5.17620499254735,
8.2102353362651));
#128427=CARTESIAN_POINT('Ctrl Pts',(-23.4072019044794,5.21134771561133,
8.35406874575578));
#128428=CARTESIAN_POINT('Ctrl Pts',(-23.4002693464821,5.25276346236797,
8.49638625049076));
#128429=CARTESIAN_POINT('Ctrl Pts',(-23.3933367884849,5.3002956501243,8.63663873446207));
#128430=CARTESIAN_POINT('Ctrl Pts',(-23.386403940659,5.34782982505307,8.77689708195206));
#128431=CARTESIAN_POINT('Ctrl Pts',(-23.3794710928331,5.40148084971533,
8.91508992173121));
#128432=CARTESIAN_POINT('Ctrl Pts',(-23.3725382450072,5.46104263992793,
9.05068448991768));
#128433=CARTESIAN_POINT('Ctrl Pts',(-23.365866417089,5.51836194431456,9.1811739580702));
#128434=CARTESIAN_POINT('Ctrl Pts',(-23.3591945891708,5.58115492638012,
9.30925697507771));
#128435=CARTESIAN_POINT('Ctrl Pts',(-23.3525227612526,5.6491961756188,9.4344770775744));
#128436=CARTESIAN_POINT('',(-23.534,5.20509380555675,8.32288496556916));
#128437=CARTESIAN_POINT('Origin',(-23.534,10.1295,7.));
#128438=CARTESIAN_POINT('Ctrl Pts',(-23.534,5.20509380555674,8.3228849655691));
#128439=CARTESIAN_POINT('Ctrl Pts',(-23.5152775845834,5.30884009368174,
8.7090779280641));
#128440=CARTESIAN_POINT('Ctrl Pts',(-23.4965551691667,5.45884546440214,
9.08275280579124));
#128441=CARTESIAN_POINT('Ctrl Pts',(-23.4778327537501,5.6497512729813,9.43417554509213));
#128442=CARTESIAN_POINT('Origin',(-26.8463464956315,10.1295,7.));
#128443=CARTESIAN_POINT('',(-21.8525208770954,5.64940737302611,9.43436256508443));
#128444=CARTESIAN_POINT('',(-21.9778242975584,5.64919617561881,9.43447707757441));
#128445=CARTESIAN_POINT('',(-26.8463464956315,5.6491961756188,9.4344770775744));
#128446=CARTESIAN_POINT('',(-23.0963464956316,10.1295667748524,12.0990157389949));
#128447=CARTESIAN_POINT('Ctrl Pts',(-23.0963464956316,10.129566778808,12.099317792417));
#128448=CARTESIAN_POINT('Ctrl Pts',(-23.0928642190133,10.2039288711016,
12.0993673408814));
#128449=CARTESIAN_POINT('Ctrl Pts',(-23.0506000607591,11.1064308613037,
12.0800148219986));
#128450=CARTESIAN_POINT('Ctrl Pts',(-22.9695540208687,12.8165649252773,
11.5744658007328));
#128451=CARTESIAN_POINT('Ctrl Pts',(-22.8532083759605,14.6458800384554,
9.78358876962574));
#128452=CARTESIAN_POINT('Ctrl Pts',(-22.7368627310523,15.4235830862095,
7.34457044966851));
#128453=CARTESIAN_POINT('Ctrl Pts',(-22.6205170861442,14.9685952857722,
4.82532064892663));
#128454=CARTESIAN_POINT('Ctrl Pts',(-22.504171441236,13.3868454525908,2.8124323194202));
#128455=CARTESIAN_POINT('Ctrl Pts',(-22.3878257963277,11.0466612589386,
1.77459151989547));
#128456=CARTESIAN_POINT('Ctrl Pts',(-22.2714801514196,8.49288304070303,
1.95345842253097));
#128457=CARTESIAN_POINT('Ctrl Pts',(-22.1551345065114,6.32026199879215,
3.30737376532056));
#128458=CARTESIAN_POINT('Ctrl Pts',(-22.0387888616032,5.03442895202576,
5.52111017618096));
#128459=CARTESIAN_POINT('Ctrl Pts',(-21.9379176517979,4.94849006028041,
7.73893242254741));
#128460=CARTESIAN_POINT('Ctrl Pts',(-21.8758283236286,5.41193861852495,
8.99675599064833));
#128461=CARTESIAN_POINT('Ctrl Pts',(-21.8525208770954,5.64940737302611,
9.43436256508443));
#128462=CARTESIAN_POINT('Ctrl Pts',(-23.3525227612526,5.6491961756188,9.4344770775744));
#128463=CARTESIAN_POINT('Ctrl Pts',(-23.3455889849682,5.7199088507827,9.56461355406351));
#128464=CARTESIAN_POINT('Ctrl Pts',(-23.3386552086839,5.79629012476817,
9.69165746727976));
#128465=CARTESIAN_POINT('Ctrl Pts',(-23.3317214323995,5.87804227441008,
9.81512134863167));
#128466=CARTESIAN_POINT('Ctrl Pts',(-23.3273446067974,5.92964689603369,
9.89305577493429));
#128467=CARTESIAN_POINT('Ctrl Pts',(-23.3229677811954,5.98339066303623,
9.96956424290311));
#128468=CARTESIAN_POINT('Ctrl Pts',(-23.3185909555933,6.03918981564711,
10.0445301108347));
#128469=CARTESIAN_POINT('Ctrl Pts',(-23.3116576154912,6.12758138927417,
10.1632837249084));
#128470=CARTESIAN_POINT('Ctrl Pts',(-23.3047242753892,6.22116338578777,
10.2782058956994));
#128471=CARTESIAN_POINT('Ctrl Pts',(-23.2977909352871,6.31957962315755,
10.3888505015891));
#128472=CARTESIAN_POINT('Ctrl Pts',(-23.2908589155155,6.41797711891765,
10.4994740371953));
#128473=CARTESIAN_POINT('Ctrl Pts',(-23.2839268957439,6.52120679919789,
10.6058213862123));
#128474=CARTESIAN_POINT('Ctrl Pts',(-23.2769948759722,6.6288732637029,10.7074807421107));
#128475=CARTESIAN_POINT('Ctrl Pts',(-23.2700626150757,6.73654347330225,
10.8091436341509));
#128476=CARTESIAN_POINT('Ctrl Pts',(-23.2631303541791,6.84865053786314,
10.9061179773461));
#128477=CARTESIAN_POINT('Ctrl Pts',(-23.2561980932826,6.96476298683125,
10.9980295943727));
#128478=CARTESIAN_POINT('Ctrl Pts',(-23.2492662087238,7.0808691323009,11.0899362217126));
#128479=CARTESIAN_POINT('Ctrl Pts',(-23.242334324165,7.20097996725737,11.1767804683626));
#128480=CARTESIAN_POINT('Ctrl Pts',(-23.2354024396062,7.32463180495121,
11.2582291399599));
#128481=CARTESIAN_POINT('Ctrl Pts',(-23.228469013263,7.44831114519013,11.3396959273071));
#128482=CARTESIAN_POINT('Ctrl Pts',(-23.2215355869198,7.57553278566342,
11.4157645597462));
#128483=CARTESIAN_POINT('Ctrl Pts',(-23.2146021605767,7.70580446372732,
11.4861454443043));
#128484=CARTESIAN_POINT('Ctrl Pts',(-23.2104832106128,7.78319513568308,
11.5279567115708));
#128485=CARTESIAN_POINT('Ctrl Pts',(-23.206364260649,7.86166171055421,11.5677615028386));
#128486=CARTESIAN_POINT('Ctrl Pts',(-23.2022453106851,7.94109688570871,
11.6055067918048));
#128487=CARTESIAN_POINT('Ctrl Pts',(-23.1953326013538,8.0744105412136,11.6688535703621));
#128488=CARTESIAN_POINT('Ctrl Pts',(-23.1884198920225,8.21050236448007,
11.7264202219746));
#128489=CARTESIAN_POINT('Ctrl Pts',(-23.1815071826912,8.34885199561309,
11.7779800841436));
#128490=CARTESIAN_POINT('Ctrl Pts',(-23.1744104587696,8.49088445926188,
11.8309124569247));
#128491=CARTESIAN_POINT('Ctrl Pts',(-23.1673137348479,8.63529628394864,
11.8775136191942));
#128492=CARTESIAN_POINT('Ctrl Pts',(-23.1602170109263,8.78150369622116,
11.9175915817602));
#128493=CARTESIAN_POINT('Ctrl Pts',(-23.1533056463726,8.92389231635461,
11.9566227478196));
#128494=CARTESIAN_POINT('Ctrl Pts',(-23.1463942818189,9.06798355227891,
11.9894671549689));
#128495=CARTESIAN_POINT('Ctrl Pts',(-23.1394829172652,9.21322389390579,
12.0159983151314));
#128496=CARTESIAN_POINT('Ctrl Pts',(-23.1322935136596,9.36430714637444,
12.0435968041202));
#128497=CARTESIAN_POINT('Ctrl Pts',(-23.125104110054,9.51663350849815,12.0643634281151));
#128498=CARTESIAN_POINT('Ctrl Pts',(-23.1179147064484,9.66956947446774,
12.0782147366652));
#128499=CARTESIAN_POINT('Ctrl Pts',(-23.1107253028428,9.82250544043734,
12.0920660452153));
#128500=CARTESIAN_POINT('Ctrl Pts',(-23.1035358992372,9.97605060390634,
12.0990020099546));
#128501=CARTESIAN_POINT('Ctrl Pts',(-23.0963464956316,10.1295667746463,
12.0989999995628));
#128502=CARTESIAN_POINT('',(-23.2216535038385,10.1296134643043,12.0989502562419));
#128503=CARTESIAN_POINT('Ctrl Pts',(-23.4778327537501,5.6497512729813,9.43417554509213));
#128504=CARTESIAN_POINT('Ctrl Pts',(-23.4577732875307,5.85429051287487,
9.81069494234303));
#128505=CARTESIAN_POINT('Ctrl Pts',(-23.3989319396752,6.59199771031906,
10.8402274681031));
#128506=CARTESIAN_POINT('Ctrl Pts',(-23.3135388565479,8.1665770620453,11.8658594947153));
#128507=CARTESIAN_POINT('Ctrl Pts',(-23.2482052396401,9.56246707210738,
12.0983697268913));
#128508=CARTESIAN_POINT('Ctrl Pts',(-23.2216535043684,10.1296134499674,
12.0988145792455));
#128509=CARTESIAN_POINT('Ctrl Pts',(-23.2216535036443,10.1296134695606,
12.0989999987375));
#128510=CARTESIAN_POINT('Ctrl Pts',(-23.2144616176573,10.2832380933687,
12.0989965800831));
#128511=CARTESIAN_POINT('Ctrl Pts',(-23.2072697316703,10.4368320308009,
12.092046129591));
#128512=CARTESIAN_POINT('Ctrl Pts',(-23.2000778456833,10.589781612833,12.0781829266863));
#128513=CARTESIAN_POINT('Ctrl Pts',(-23.1950395855473,10.6969301109268,
12.0684710899472));
#128514=CARTESIAN_POINT('Ctrl Pts',(-23.1900013254114,10.80376240697,12.0553677903385));
#128515=CARTESIAN_POINT('Ctrl Pts',(-23.1849630652754,10.9100690396704,
12.0388999766128));
#128516=CARTESIAN_POINT('Ctrl Pts',(-23.1780322210911,11.0563089493057,
12.016246154081));
#128517=CARTESIAN_POINT('Ctrl Pts',(-23.1711013769068,11.2015880256627,
11.9872177039362));
#128518=CARTESIAN_POINT('Ctrl Pts',(-23.1641705327225,11.3453457830432,
11.9519208426484));
#128519=CARTESIAN_POINT('Ctrl Pts',(-23.1572410393046,11.4890755231802,
11.9166308604382));
#128520=CARTESIAN_POINT('Ctrl Pts',(-23.1503115458867,11.6312842144825,
11.875074983332));
#128521=CARTESIAN_POINT('Ctrl Pts',(-23.1433820524688,11.7714233688928,
11.8274101390584));
#128522=CARTESIAN_POINT('Ctrl Pts',(-23.1364523390414,11.9115669726828,
11.779743781439));
#128523=CARTESIAN_POINT('Ctrl Pts',(-23.129522625614,12.0496405935019,11.725968171853));
#128524=CARTESIAN_POINT('Ctrl Pts',(-23.1225929121865,12.1851121473728,
11.666289714492));
#128525=CARTESIAN_POINT('Ctrl Pts',(-23.1156635809782,12.3205762291,11.6066145487888));
#128526=CARTESIAN_POINT('Ctrl Pts',(-23.1087342497699,12.453438228391,11.5410373210932));
#128527=CARTESIAN_POINT('Ctrl Pts',(-23.1018049185616,12.5831872350453,
11.4698120712817));
#128528=CARTESIAN_POINT('Ctrl Pts',(-23.0948740323597,12.7129653583441,
11.3985708379931));
#128529=CARTESIAN_POINT('Ctrl Pts',(-23.0879431461578,12.8396288027836,
11.3216792094331));
#128530=CARTESIAN_POINT('Ctrl Pts',(-23.0810122599559,12.9626918508012,
11.2394368654992));
#128531=CARTESIAN_POINT('Ctrl Pts',(-23.0768806467596,13.0360517211474,
11.1904108760966));
#128532=CARTESIAN_POINT('Ctrl Pts',(-23.0727490335634,13.1081326835169,
11.1394843440002));
#128533=CARTESIAN_POINT('Ctrl Pts',(-23.0686174203672,13.1788367906057,
11.0867280478958));
#128534=CARTESIAN_POINT('Ctrl Pts',(-23.0616832477982,13.2975009676742,
10.9981860562044));
#128535=CARTESIAN_POINT('Ctrl Pts',(-23.0547490752291,13.4123264715572,
10.9044570184215));
#128536=CARTESIAN_POINT('Ctrl Pts',(-23.0478149026601,13.5228675281008,
10.8058977678376));
#128537=CARTESIAN_POINT('Ctrl Pts',(-23.0408820410097,13.6333876866445,
10.7073571500701));
#128538=CARTESIAN_POINT('Ctrl Pts',(-23.0339491793593,13.7396247673742,
10.6039883612046));
#128539=CARTESIAN_POINT('Ctrl Pts',(-23.027016317709,13.8411673613832,10.4961874089417));
#128540=CARTESIAN_POINT('Ctrl Pts',(-23.0200832090312,13.9427135734955,
10.3883826155816));
#128541=CARTESIAN_POINT('Ctrl Pts',(-23.0131501003533,14.0395647351762,
10.2761455810761));
#128542=CARTESIAN_POINT('Ctrl Pts',(-23.0062169916755,14.131347111674,10.1599083364532));
#128543=CARTESIAN_POINT('Ctrl Pts',(-22.9992842580324,14.2231245233599,
10.0436773794868));
#128544=CARTESIAN_POINT('Ctrl Pts',(-22.9923515243894,14.3098334944501,
9.9234469053268));
#128545=CARTESIAN_POINT('Ctrl Pts',(-22.9854187907463,14.3911413124602,
9.79968111111478));
#128546=CARTESIAN_POINT('Ctrl Pts',(-22.9784845207415,14.4724671490789,
9.67588788919075));
#128547=CARTESIAN_POINT('Ctrl Pts',(-22.9715502507368,14.5483892594452,
9.54855805804282));
#128548=CARTESIAN_POINT('Ctrl Pts',(-22.9646159807321,14.6186185668019,
9.41818433813362));
#128549=CARTESIAN_POINT('Ctrl Pts',(-22.960501245641,14.6602920227245,9.34082171454237));
#128550=CARTESIAN_POINT('Ctrl Pts',(-22.95638651055,14.6999618159018,9.26238781469777));
#128551=CARTESIAN_POINT('Ctrl Pts',(-22.952271775459,14.7375752110852,9.18298965846895));
#128552=CARTESIAN_POINT('Ctrl Pts',(-22.9453381247487,14.800956726167,9.04919755031274));
#128553=CARTESIAN_POINT('Ctrl Pts',(-22.9384044740384,14.8585183931822,
8.91262019456305));
#128554=CARTESIAN_POINT('Ctrl Pts',(-22.9314708233281,14.9100334467114,
8.77378154372893));
#128555=CARTESIAN_POINT('Ctrl Pts',(-22.92453848664,14.9615387374293,8.63496920472942));
#128556=CARTESIAN_POINT('Ctrl Pts',(-22.917606149952,15.0069995860105,8.49389673540899));
#128557=CARTESIAN_POINT('Ctrl Pts',(-22.9106738132639,15.0462379353463,
8.35110661131037));
#128558=CARTESIAN_POINT('Ctrl Pts',(-22.9037412290525,15.085477685711,8.20831138880432));
#128559=CARTESIAN_POINT('Ctrl Pts',(-22.8968086448412,15.1184944014449,
8.06379870665251));
#128560=CARTESIAN_POINT('Ctrl Pts',(-22.8898760606299,15.1451601822359,
7.91812522911281));
#128561=CARTESIAN_POINT('Ctrl Pts',(-22.8829438499011,15.1718245264478,
7.77245959951431));
#128562=CARTESIAN_POINT('Ctrl Pts',(-22.8760116391724,15.1921385617596,
7.62563362499968));
#128563=CARTESIAN_POINT('Ctrl Pts',(-22.8690794284437,15.2060256970908,
7.47821318130803));
#128564=CARTESIAN_POINT('Ctrl Pts',(-22.8621456743553,15.2199159241982,
7.33075991651844));
#128565=CARTESIAN_POINT('Ctrl Pts',(-22.855211920267,15.2273763612686,7.18271224732234));
#128566=CARTESIAN_POINT('Ctrl Pts',(-22.8482781661786,15.2283823298558,
7.03464081817565));
#128567=CARTESIAN_POINT('Ctrl Pts',(-22.8441608209693,15.2289796859043,
6.9467142517509));
#128568=CARTESIAN_POINT('Ctrl Pts',(-22.8400434757601,15.2273021079282,
6.85877936703632));
#128569=CARTESIAN_POINT('Ctrl Pts',(-22.8359261305508,15.223353127859,6.77095565538246));
#128570=CARTESIAN_POINT('Ctrl Pts',(-22.8289927904143,15.2167033036104,
6.62306626695431));
#128571=CARTESIAN_POINT('Ctrl Pts',(-22.8220594502778,15.2036075003542,
6.47544108085083));
#128572=CARTESIAN_POINT('Ctrl Pts',(-22.8151261101414,15.1841106766401,
6.32864919185574));
#128573=CARTESIAN_POINT('Ctrl Pts',(-22.8081940903344,15.1646175657443,
6.18188525672731));
#128574=CARTESIAN_POINT('Ctrl Pts',(-22.8012620705275,15.1387259098974,
6.03595462967193));
#128575=CARTESIAN_POINT('Ctrl Pts',(-22.7943300507205,15.1065323796292,
5.8914199658471));
#128576=CARTESIAN_POINT('Ctrl Pts',(-22.7873977897876,15.0743377295293,
5.74688027447465));
#128577=CARTESIAN_POINT('Ctrl Pts',(-22.7804655288547,15.0358408349672,
5.60373696693589));
#128578=CARTESIAN_POINT('Ctrl Pts',(-22.7735332679218,14.9911893286948,
5.46254174975221));
#128579=CARTESIAN_POINT('Ctrl Pts',(-22.7666013833261,14.9465402464547,
5.32135419774698));
#128580=CARTESIAN_POINT('Ctrl Pts',(-22.7596694987304,14.8957373216521,
5.18211483944176));
#128581=CARTESIAN_POINT('Ctrl Pts',(-22.7527376141347,14.8389778369684,
5.04535949517476));
#128582=CARTESIAN_POINT('Ctrl Pts',(-22.7458041877542,14.7822057278808,
4.9085737338822));
#128583=CARTESIAN_POINT('Ctrl Pts',(-22.7388707613737,14.7194745384637,
4.77427339605927));
#128584=CARTESIAN_POINT('Ctrl Pts',(-22.7319373349933,14.6510296539597,
4.64297420710704));
#128585=CARTESIAN_POINT('Ctrl Pts',(-22.7278183852097,14.6103685108622,
4.56497312420261));
#128586=CARTESIAN_POINT('Ctrl Pts',(-22.7236994354262,14.5676917913382,
4.48803079706271));
#128587=CARTESIAN_POINT('Ctrl Pts',(-22.7195804856426,14.5230586438665,
4.4122512790253));
#128588=CARTESIAN_POINT('Ctrl Pts',(-22.7126467716635,14.4479245696929,
4.28468635807346));
#128589=CARTESIAN_POINT('Ctrl Pts',(-22.7057130576844,14.3672181376313,
4.16037390646582));
#128590=CARTESIAN_POINT('Ctrl Pts',(-22.6987793437054,14.2812456294001,
4.03979574543294));
#128591=CARTESIAN_POINT('Ctrl Pts',(-22.6918469440267,14.1952894174433,
3.91924044025052));
#128592=CARTESIAN_POINT('Ctrl Pts',(-22.6849145443481,14.1040693126661,
3.8024182823838));
#128593=CARTESIAN_POINT('Ctrl Pts',(-22.6779821446695,14.0079342710063,
3.68978118465205));
#128594=CARTESIAN_POINT('Ctrl Pts',(-22.6710494985103,13.9117958112779,
3.57714008212316));
#128595=CARTESIAN_POINT('Ctrl Pts',(-22.6641168523511,13.810742277035,3.4686845910636));
#128596=CARTESIAN_POINT('Ctrl Pts',(-22.6571842061919,13.7051625248584,
3.36483308384289));
#128597=CARTESIAN_POINT('Ctrl Pts',(-22.6502519342582,13.5995884718967,
3.26098718254614));
#128598=CARTESIAN_POINT('Ctrl Pts',(-22.6433196623246,13.4894889262164,
3.16174499892527));
#128599=CARTESIAN_POINT('Ctrl Pts',(-22.6363873903909,13.375289173411,3.06748761708652));
#128600=CARTESIAN_POINT('Ctrl Pts',(-22.6294535767895,13.2610640237249,
2.97320927335051));
#128601=CARTESIAN_POINT('Ctrl Pts',(-22.622519763188,13.1427370999496,2.88391815695374));
#128602=CARTESIAN_POINT('Ctrl Pts',(-22.6155859495865,13.0207667789116,
2.79995507010194));
#128603=CARTESIAN_POINT('Ctrl Pts',(-22.6114689133025,12.9483454151206,
2.7501009645609));
#128604=CARTESIAN_POINT('Ctrl Pts',(-22.6073518770184,12.8746401652181,
2.70212448718511));
#128605=CARTESIAN_POINT('Ctrl Pts',(-22.6032348407344,12.7997518707891,
2.65608978608592));
#128606=CARTESIAN_POINT('Ctrl Pts',(-22.5963013561296,12.6736327888376,
2.57856292711801));
#128607=CARTESIAN_POINT('Ctrl Pts',(-22.5893678715248,12.5441133362429,
2.50651890621843));
#128608=CARTESIAN_POINT('Ctrl Pts',(-22.5824343869199,12.4116897238054,
2.4402400211681));
#128609=CARTESIAN_POINT('Ctrl Pts',(-22.5755022202333,12.2792912824762,
2.37397373442229));
#128610=CARTESIAN_POINT('Ctrl Pts',(-22.5685700535467,12.1439900781449,
2.31347054505179));
#128611=CARTESIAN_POINT('Ctrl Pts',(-22.5616378868601,12.0063060236781,
2.25896634166285));
#128612=CARTESIAN_POINT('Ctrl Pts',(-22.5547054768533,11.8686171364781,
2.20446022516737));
#128613=CARTESIAN_POINT('Ctrl Pts',(-22.5477730668465,11.7285455379248,
2.15595364079637));
#128614=CARTESIAN_POINT('Ctrl Pts',(-22.5408406568397,11.5866306909856,
2.11363415723017));
#128615=CARTESIAN_POINT('Ctrl Pts',(-22.5339086222827,11.4447235299589,
2.07131696562882));
#128616=CARTESIAN_POINT('Ctrl Pts',(-22.5269765877257,11.3009736373841,
2.03518629791229));
#128617=CARTESIAN_POINT('Ctrl Pts',(-22.5200445531686,11.1559352036829,
2.00537971687132));
#128618=CARTESIAN_POINT('Ctrl Pts',(-22.5131109767612,11.0108645099632,
1.97556650613344));
#128619=CARTESIAN_POINT('Ctrl Pts',(-22.5061774003538,10.864505026392,1.95208025927438));
#128620=CARTESIAN_POINT('Ctrl Pts',(-22.4992438239464,10.7174213194625,
1.9350074509313));
#128621=CARTESIAN_POINT('Ctrl Pts',(-22.495125614573,10.6300607042531,1.92486702768973));
#128622=CARTESIAN_POINT('Ctrl Pts',(-22.4910074051996,10.5424447657293,
1.91698814828052));
#128623=CARTESIAN_POINT('Ctrl Pts',(-22.4868891958262,10.4546927511912,
1.9113802780545));
#128624=CARTESIAN_POINT('Ctrl Pts',(-22.4799556232166,10.3069501501543,
1.90193865625436));
#128625=CARTESIAN_POINT('Ctrl Pts',(-22.4730220506069,10.158770604134,1.89893406224141));
#128626=CARTESIAN_POINT('Ctrl Pts',(-22.4660884779973,10.0107247644674,
1.90238355273524));
#128627=CARTESIAN_POINT('Ctrl Pts',(-22.4591562216396,9.86270702945001,
1.90583238838649));
#128628=CARTESIAN_POINT('Ctrl Pts',(-22.4522239652819,9.71482328045241,
1.91573285633567));
#128629=CARTESIAN_POINT('Ctrl Pts',(-22.4452917089242,9.56764337792384,
1.93204990787901));
#128630=CARTESIAN_POINT('Ctrl Pts',(-22.4383592076211,9.420458274917,1.94836753597166));
#128631=CARTESIAN_POINT('Ctrl Pts',(-22.4314267063179,9.27397739706878,
1.97110216823797));
#128632=CARTESIAN_POINT('Ctrl Pts',(-22.4244942050148,9.12876525084503,
2.00016690660241));
#128633=CARTESIAN_POINT('Ctrl Pts',(-22.41756207846,8.98356095431581,2.02923007382199));
#128634=CARTESIAN_POINT('Ctrl Pts',(-22.4106299519053,8.83962557614821,
2.06462259662998));
#128635=CARTESIAN_POINT('Ctrl Pts',(-22.4036978253505,8.69751321817358,
2.10620649631859));
#128636=CARTESIAN_POINT('Ctrl Pts',(-22.3967641566674,8.55536924572963,
2.14779964680663));
#128637=CARTESIAN_POINT('Ctrl Pts',(-22.3898304879842,8.41504942121115,
2.19558683341147));
#128638=CARTESIAN_POINT('Ctrl Pts',(-22.3828968193011,8.27709309039585,
2.24938007821602));
#128639=CARTESIAN_POINT('Ctrl Pts',(-22.3787790631734,8.19516380410787,
2.28132672486794));
#128640=CARTESIAN_POINT('Ctrl Pts',(-22.3746613070457,8.11406779091711,
2.31539071346896));
#128641=CARTESIAN_POINT('Ctrl Pts',(-22.370543550918,8.03391480971792,2.35152458215918));
#128642=CARTESIAN_POINT('Ctrl Pts',(-22.3636099925257,7.89895165060084,
2.41236749775123));
#128643=CARTESIAN_POINT('Ctrl Pts',(-22.3566764341333,7.76661674914673,
2.47910262080128));
#128644=CARTESIAN_POINT('Ctrl Pts',(-22.3497428757409,7.63742230671767,
2.55147779924112));
#128645=CARTESIAN_POINT('Ctrl Pts',(-22.3428106342854,7.5082524030468,2.62383923098281));
#128646=CARTESIAN_POINT('Ctrl Pts',(-22.3358783928298,7.3822220565691,2.70183841932422));
#128647=CARTESIAN_POINT('Ctrl Pts',(-22.3289461513742,7.25981836998035,
2.78517754320212));
#128648=CARTESIAN_POINT('Ctrl Pts',(-22.322013665852,7.13741037386829,2.86851960123916));
#128649=CARTESIAN_POINT('Ctrl Pts',(-22.3150811803298,7.01862956828097,
2.95720178773977));
#128650=CARTESIAN_POINT('Ctrl Pts',(-22.3081486948075,6.90393404520842,
3.05088297574135));
#128651=CARTESIAN_POINT('Ctrl Pts',(-22.3012165844928,6.78924472981139,
3.14455909342806));
#128652=CARTESIAN_POINT('Ctrl Pts',(-22.2942844741781,6.67864050993959,
3.24323346137456));
#128653=CARTESIAN_POINT('Ctrl Pts',(-22.2873523638634,6.5725463642529,3.34652469104477));
#128654=CARTESIAN_POINT('Ctrl Pts',(-22.2804187119845,6.4664286253275,3.44983889064064));
#128655=CARTESIAN_POINT('Ctrl Pts',(-22.2734850601056,6.36482320156598,
3.55777177275135));
#128656=CARTESIAN_POINT('Ctrl Pts',(-22.2665514082267,6.2681186198229,3.66990468052016));
#128657=CARTESIAN_POINT('Ctrl Pts',(-22.2624335741544,6.21068663035953,
3.73649941534445));
#128658=CARTESIAN_POINT('Ctrl Pts',(-22.2583157400821,6.15498248326484,
3.80457483855878));
#128659=CARTESIAN_POINT('Ctrl Pts',(-22.2541979060098,6.10108093818732,
3.87403761020318));
#128660=CARTESIAN_POINT('Ctrl Pts',(-22.247264295271,6.01032149396891,3.99099905424433));
#128661=CARTESIAN_POINT('Ctrl Pts',(-22.2403306845322,5.92464363472474,
4.11193600283431));
#128662=CARTESIAN_POINT('Ctrl Pts',(-22.2333970737934,5.84438185374589,
4.23638579525945));
#128663=CARTESIAN_POINT('Ctrl Pts',(-22.2264647793601,5.76413530999738,
4.36081196161838));
#128664=CARTESIAN_POINT('Ctrl Pts',(-22.2195324849268,5.68930297214713,
4.48874936360589));
#128665=CARTESIAN_POINT('Ctrl Pts',(-22.2126001904935,5.62017577060433,
4.61970674197797));
#128666=CARTESIAN_POINT('Ctrl Pts',(-22.2056676515668,5.55104613103073,
4.75066873905461));
#128667=CARTESIAN_POINT('Ctrl Pts',(-22.1987351126401,5.48762218766616,
4.88465063487431));
#128668=CARTESIAN_POINT('Ctrl Pts',(-22.1918025737133,5.43014895812622,
5.02113649150837));
#128669=CARTESIAN_POINT('Ctrl Pts',(-22.1848704098817,5.37267883825905,
5.15761496337642));
#128670=CARTESIAN_POINT('Ctrl Pts',(-22.1779382460501,5.3211589153847,5.2965968199325));
#128671=CARTESIAN_POINT('Ctrl Pts',(-22.1710060822185,5.27578609499789,
5.43754605559421));
#128672=CARTESIAN_POINT('Ctrl Pts',(-22.1640723771204,5.23040318662025,
5.57852662928132));
#128673=CARTESIAN_POINT('Ctrl Pts',(-22.1571386720224,5.19117021294783,
5.72147514131237));
#128674=CARTESIAN_POINT('Ctrl Pts',(-22.1502049669243,5.15823441927751,
5.8658397265272));
#128675=CARTESIAN_POINT('Ctrl Pts',(-22.1460873983168,5.13867555599091,
5.95157038217522));
#128676=CARTESIAN_POINT('Ctrl Pts',(-22.1419698297092,5.12133647341795,
6.03780015164788));
#128677=CARTESIAN_POINT('Ctrl Pts',(-22.1378522611016,5.10623951371014,
6.12441157677879));
#128678=CARTESIAN_POINT('Ctrl Pts',(-22.1309189485113,5.08081870089726,
6.27025106157069));
#128679=CARTESIAN_POINT('Ctrl Pts',(-22.123985635921,5.06174897458694,6.41722355017293));
#128680=CARTESIAN_POINT('Ctrl Pts',(-22.1170523233307,5.04910923496427,
6.56476365668796));
#128681=CARTESIAN_POINT('Ctrl Pts',(-22.1101203285711,5.03647189780609,
6.71227571991428));
#128682=CARTESIAN_POINT('Ctrl Pts',(-22.1031883338116,5.03026213714831,
6.86035485655778));
#128683=CARTESIAN_POINT('Ctrl Pts',(-22.096256339052,5.03050696985794,7.00843081032557));
#128684=CARTESIAN_POINT('Ctrl Pts',(-22.0893240991684,5.03075181122517,
7.1565120002449));
#128685=CARTESIAN_POINT('Ctrl Pts',(-22.0823918592848,5.03745170547962,
7.3045896764382));
#128686=CARTESIAN_POINT('Ctrl Pts',(-22.0754596194012,5.05058154531324,
7.45209327648424));
#128687=CARTESIAN_POINT('Ctrl Pts',(-22.0685277535374,5.06371067674367,
7.59958891816818));
#128688=CARTESIAN_POINT('Ctrl Pts',(-22.0615958876737,5.08326902931617,
7.74651021643174));
#128689=CARTESIAN_POINT('Ctrl Pts',(-22.0546640218099,5.1091795875243,7.89229140760168));
#128690=CARTESIAN_POINT('Ctrl Pts',(-22.0477306104145,5.13509592276123,
8.03810510220653));
#128691=CARTESIAN_POINT('Ctrl Pts',(-22.0407971990191,5.16736723568734,
8.18277785615113));
#128692=CARTESIAN_POINT('Ctrl Pts',(-22.0338637876236,5.20586520532838,
8.32575314772358));
#128693=CARTESIAN_POINT('Ctrl Pts',(-22.0297447304802,5.22873639063855,
8.41069306582364));
#128694=CARTESIAN_POINT('Ctrl Pts',(-22.0256256733368,5.2538042436447,8.49503408736315));
#128695=CARTESIAN_POINT('Ctrl Pts',(-22.0215066161934,5.28103345893842,
8.57866183845887));
#128696=CARTESIAN_POINT('Ctrl Pts',(-22.0142262297542,5.32916078586583,
8.72647293304141));
#128697=CARTESIAN_POINT('Ctrl Pts',(-22.0069458433151,5.3840610914241,8.87210820405202));
#128698=CARTESIAN_POINT('Ctrl Pts',(-21.9996654568759,5.44550712798327,
9.01494708985037));
#128699=CARTESIAN_POINT('Ctrl Pts',(-21.9923850704367,5.50695316454245,
9.15778597564872));
#128700=CARTESIAN_POINT('Ctrl Pts',(-21.9851046839976,5.57494477387249,
9.29782808536408));
#128701=CARTESIAN_POINT('Ctrl Pts',(-21.9778242975584,5.64919617561881,
9.43447707757441));
#128702=CARTESIAN_POINT('Origin',(-26.8463464956315,10.1295,7.));
#128703=CARTESIAN_POINT('',(-20.35256332674,5.6491961756188,9.4344770775744));
#128704=CARTESIAN_POINT('',(-20.4776000298804,5.6491961756188,9.4344770775744));
#128705=CARTESIAN_POINT('',(-26.8463464956315,5.6491961756188,9.4344770775744));
#128706=CARTESIAN_POINT('',(-21.5963464956315,10.1291161856969,12.0989999855547));
#128707=CARTESIAN_POINT('Ctrl Pts',(-21.5963464956315,10.1291161856969,
12.0989999855547));
#128708=CARTESIAN_POINT('Ctrl Pts',(-21.5886997577445,10.2924291785527,
12.0990122785264));
#128709=CARTESIAN_POINT('Ctrl Pts',(-21.5810530198574,10.4557419617455,
12.0911739196201));
#128710=CARTESIAN_POINT('Ctrl Pts',(-21.5734062819704,10.6183440341081,
12.0755130292727));
#128711=CARTESIAN_POINT('Ctrl Pts',(-21.5666848517297,10.761270142277,12.0617472138972));
#128712=CARTESIAN_POINT('Ctrl Pts',(-21.5599634214889,10.9036700321504,
12.0419345290273));
#128713=CARTESIAN_POINT('Ctrl Pts',(-21.5532419912482,11.0450086188271,
12.0161384519223));
#128714=CARTESIAN_POINT('Ctrl Pts',(-21.5465222109883,11.1863125096208,
11.9903487072541));
#128715=CARTESIAN_POINT('Ctrl Pts',(-21.5398024307283,11.3265552547391,
11.9585785632498));
#128716=CARTESIAN_POINT('Ctrl Pts',(-21.5330826504684,11.4652102525116,
11.9209429097822));
#128717=CARTESIAN_POINT('Ctrl Pts',(-21.5263615518046,11.6038924540449,
11.8832998722942));
#128718=CARTESIAN_POINT('Ctrl Pts',(-21.5196404531407,11.7409859290593,
11.8397891166586));
#128719=CARTESIAN_POINT('Ctrl Pts',(-21.5129193544769,11.8759772620419,
11.7905759750964));
#128720=CARTESIAN_POINT('Ctrl Pts',(-21.5061977698631,12.0109783551886,
11.7413592753181));
#128721=CARTESIAN_POINT('Ctrl Pts',(-21.4994761852493,12.1438766594992,
11.6864394991817));
#128722=CARTESIAN_POINT('Ctrl Pts',(-21.4927546006356,12.2741773917404,
11.6260306835729));
#128723=CARTESIAN_POINT('Ctrl Pts',(-21.4860285543178,12.4045646159827,
11.5655817693456));
#128724=CARTESIAN_POINT('Ctrl Pts',(-21.479302508,12.5323504905475,11.4996366941743));
#128725=CARTESIAN_POINT('Ctrl Pts',(-21.4725764616822,12.6570630553875,
11.4284563903284));
#128726=CARTESIAN_POINT('Ctrl Pts',(-21.4674045201422,12.7529598221028,
11.3737228436212));
#128727=CARTESIAN_POINT('Ctrl Pts',(-21.4622325786022,12.8470398696579,
11.3158948186789));
#128728=CARTESIAN_POINT('Ctrl Pts',(-21.4570606370622,12.9390999696984,
11.255108577965));
#128729=CARTESIAN_POINT('Ctrl Pts',(-21.4497817937609,13.0686627339555,
11.1695597530969));
#128730=CARTESIAN_POINT('Ctrl Pts',(-21.4425029504596,13.1943036068353,
11.0780978347688));
#128731=CARTESIAN_POINT('Ctrl Pts',(-21.4352241071583,13.3155153827349,
10.9810936915597));
#128732=CARTESIAN_POINT('Ctrl Pts',(-21.427946142148,13.4367125327922,10.8841012532143));
#128733=CARTESIAN_POINT('Ctrl Pts',(-21.4206681771377,13.553481456089,10.7815680846603));
#128734=CARTESIAN_POINT('Ctrl Pts',(-21.4133902121274,13.6653475008962,
10.6739057487102));
#128735=CARTESIAN_POINT('Ctrl Pts',(-21.4061165971437,13.7771466835695,
10.5663077623448));
#128736=CARTESIAN_POINT('Ctrl Pts',(-21.39884298216,13.884048659969,10.4535869088841));
#128737=CARTESIAN_POINT('Ctrl Pts',(-21.3915693671764,13.9856148483401,
10.3361923320473));
#128738=CARTESIAN_POINT('Ctrl Pts',(-21.3843006041387,14.0871132858521,
10.2188760645726));
#128739=CARTESIAN_POINT('Ctrl Pts',(-21.377031841101,14.1832828744343,10.0968924881681));
#128740=CARTESIAN_POINT('Ctrl Pts',(-21.3697630780634,14.2737238199281,
9.97072548889001));
#128741=CARTESIAN_POINT('Ctrl Pts',(-21.362503319337,14.3640527300697,9.8447147812575));
#128742=CARTESIAN_POINT('Ctrl Pts',(-21.3552435606107,14.4486670178919,
9.714531202894));
#128743=CARTESIAN_POINT('Ctrl Pts',(-21.3479838018843,14.5272087473904,
9.58068959255577));
#128744=CARTESIAN_POINT('Ctrl Pts',(-21.3455608653075,14.5534219641621,
9.53602010071664));
#128745=CARTESIAN_POINT('Ctrl Pts',(-21.3431379287308,14.5789591128104,
9.49094340429971));
#128746=CARTESIAN_POINT('Ctrl Pts',(-21.340714992154,14.6038079371955,9.44547939740844));
#128747=CARTESIAN_POINT('Ctrl Pts',(-21.3339843753385,14.6728348844358,
9.31918603413387));
#128748=CARTESIAN_POINT('Ctrl Pts',(-21.3272537585231,14.7365235713096,
9.18994468860563));
#128749=CARTESIAN_POINT('Ctrl Pts',(-21.3205231417076,14.7946316255851,
9.05823903275727));
#128750=CARTESIAN_POINT('Ctrl Pts',(-21.3137927443259,14.8527377854031,
8.92653767081916));
#128751=CARTESIAN_POINT('Ctrl Pts',(-21.3070623469442,14.9052635284588,
8.79237249361529));
#128752=CARTESIAN_POINT('Ctrl Pts',(-21.3003319495625,14.9520141566814,
8.65624823278624));
#128753=CARTESIAN_POINT('Ctrl Pts',(-21.2935981100412,14.9987886946641,
8.5200543536752));
#128754=CARTESIAN_POINT('Ctrl Pts',(-21.2868642705199,15.0397820953061,
8.38189973457288));
#128755=CARTESIAN_POINT('Ctrl Pts',(-21.2801304309986,15.0748490349448,
8.24230588929219));
#128756=CARTESIAN_POINT('Ctrl Pts',(-21.2733949256714,15.1099246493845,
8.10267751151975));
#128757=CARTESIAN_POINT('Ctrl Pts',(-21.2666594203442,15.1390707988719,
7.96160955465822));
#128758=CARTESIAN_POINT('Ctrl Pts',(-21.259923915017,15.1621931252001,7.81963461832902));
#128759=CARTESIAN_POINT('Ctrl Pts',(-21.253182158197,15.185336912287,7.67752790936546));
#128760=CARTESIAN_POINT('Ctrl Pts',(-21.2464404013771,15.2024456529539,
7.53451290148192));
#128761=CARTESIAN_POINT('Ctrl Pts',(-21.2396986445571,15.2134767052048,
7.39112895691197));
#128762=CARTESIAN_POINT('Ctrl Pts',(-21.2345888787867,15.2218374477693,
7.28245426104793));
#128763=CARTESIAN_POINT('Ctrl Pts',(-21.2294791130162,15.2267078994303,
7.17356777436155));
#128764=CARTESIAN_POINT('Ctrl Pts',(-21.2243693472458,15.2280894461353,
7.06470440292566));
#128765=CARTESIAN_POINT('Ctrl Pts',(-21.2176534076632,15.229905260131,6.92162155761189));
#128766=CARTESIAN_POINT('Ctrl Pts',(-21.2109374680805,15.2256953339438,
6.77833302577364));
#128767=CARTESIAN_POINT('Ctrl Pts',(-21.2042215284979,15.2154462623456,
6.63537469021888));
#128768=CARTESIAN_POINT('Ctrl Pts',(-21.19751094786,15.2052053689341,6.49253042743137));
#128769=CARTESIAN_POINT('Ctrl Pts',(-21.1908003672221,15.1889349545926,
6.35001620351518));
#128770=CARTESIAN_POINT('Ctrl Pts',(-21.1840897865841,15.1666736682128,
6.20836723396308));
#128771=CARTESIAN_POINT('Ctrl Pts',(-21.1773831930339,15.1444256083638,
6.06680242506643));
#128772=CARTESIAN_POINT('Ctrl Pts',(-21.1706765994837,15.1161938245229,
5.9261022107914));
#128773=CARTESIAN_POINT('Ctrl Pts',(-21.1639700059334,15.0820687172022,
5.7867959358006));
#128774=CARTESIAN_POINT('Ctrl Pts',(-21.1572660310837,15.0479569345949,
5.64754405525195));
#128775=CARTESIAN_POINT('Ctrl Pts',(-21.150562056234,15.0079565014168,5.50968538809937));
#128776=CARTESIAN_POINT('Ctrl Pts',(-21.1438580813843,14.9622087395493,
5.37373826255313));
#128777=CARTESIAN_POINT('Ctrl Pts',(-21.1371540388033,14.9164605154848,
5.23778976351097));
#128778=CARTESIAN_POINT('Ctrl Pts',(-21.1304499962222,14.8649649559917,
5.10375319788511));
#128779=CARTESIAN_POINT('Ctrl Pts',(-21.1237459536412,14.8079130727842,
4.97213113826322));
#128780=CARTESIAN_POINT('Ctrl Pts',(-21.1170415605953,14.7508582070962,
4.84050219788285));
#128781=CARTESIAN_POINT('Ctrl Pts',(-21.1103371675495,14.6882465856708,
4.71128835456374));
#128782=CARTESIAN_POINT('Ctrl Pts',(-21.1036327745036,14.6203170020036,
4.58497129323161));
#128783=CARTESIAN_POINT('Ctrl Pts',(-21.0969267918465,14.5523713122353,
4.45862428213015));
#128784=CARTESIAN_POINT('Ctrl Pts',(-21.0902208091894,14.479105323588,4.33517574698731));
#128785=CARTESIAN_POINT('Ctrl Pts',(-21.0835148265322,14.4008032643884,
4.21508179229178));
#128786=CARTESIAN_POINT('Ctrl Pts',(-21.0768060142702,14.322468165454,4.09493716367445));
#128787=CARTESIAN_POINT('Ctrl Pts',(-21.0700972020082,14.2390929647963,
3.97815024480523));
#128788=CARTESIAN_POINT('Ctrl Pts',(-21.0633883897462,14.1510045080489,
3.86514713395636));
#128789=CARTESIAN_POINT('Ctrl Pts',(-21.0566716293294,14.0628116899532,
3.75201014453292));
#128790=CARTESIAN_POINT('Ctrl Pts',(-21.0499548689125,13.9698946892751,
3.6426662096424));
#128791=CARTESIAN_POINT('Ctrl Pts',(-21.0432381084957,13.8726203565898,
3.53750797891421));
#128792=CARTESIAN_POINT('Ctrl Pts',(-21.0365169651504,13.7752825488948,
3.43228112864843));
#128793=CARTESIAN_POINT('Ctrl Pts',(-21.0297958218052,13.6735820019257,
3.33124568889817));
#128794=CARTESIAN_POINT('Ctrl Pts',(-21.02307467846,13.5679211722343,3.23475620413089));
#128795=CARTESIAN_POINT('Ctrl Pts',(-21.0163436137068,13.4621043714322,
3.13812428652298));
#128796=CARTESIAN_POINT('Ctrl Pts',(-21.0096125489537,13.3523158907957,
3.04605196896882));
#128797=CARTESIAN_POINT('Ctrl Pts',(-21.0028814842005,13.238990562671,2.95885295483325));
#128798=CARTESIAN_POINT('Ctrl Pts',(-20.9991470086101,13.1761163091654,
2.91047389420382));
#128799=CARTESIAN_POINT('Ctrl Pts',(-20.9954125330198,13.112153873401,2.86359414379601));
#128800=CARTESIAN_POINT('Ctrl Pts',(-20.9916780574294,13.0471810287064,
2.81826131678142));
#128801=CARTESIAN_POINT('Ctrl Pts',(-20.9851848243432,12.9342109972609,
2.73943991197113));
#128802=CARTESIAN_POINT('Ctrl Pts',(-20.978691591257,12.8178257484995,2.66504726072126));
#128803=CARTESIAN_POINT('Ctrl Pts',(-20.9721983581708,12.6984140612852,
2.59540222656695));
#128804=CARTESIAN_POINT('Ctrl Pts',(-20.9657135848688,12.5791579509766,
2.52584793025557));
#128805=CARTESIAN_POINT('Ctrl Pts',(-20.9592288115668,12.4568835846724,
2.46102915145827));
#128806=CARTESIAN_POINT('Ctrl Pts',(-20.9527440382649,12.3320115771825,
2.40122366793327));
#128807=CARTESIAN_POINT('Ctrl Pts',(-20.9462660723299,12.2072706536237,
2.34148096499489));
#128808=CARTESIAN_POINT('Ctrl Pts',(-20.9397881063949,12.0799378707497,
2.2867412629917));
#128809=CARTESIAN_POINT('Ctrl Pts',(-20.9333101404599,11.9504610849393,
2.23723801485559));
#128810=CARTESIAN_POINT('Ctrl Pts',(-20.9268373376134,11.8210874951179,
2.1877742219517));
#128811=CARTESIAN_POINT('Ctrl Pts',(-20.9203645347668,11.6895736743514,
2.14353872349908));
#128812=CARTESIAN_POINT('Ctrl Pts',(-20.9138917319203,11.5563897947106,
2.10471793317782));
#128813=CARTESIAN_POINT('Ctrl Pts',(-20.9074218424765,11.4232658610135,
2.06591461605917));
#128814=CARTESIAN_POINT('Ctrl Pts',(-20.9009519530327,11.2884737466312,
2.03252127528892));
#128815=CARTESIAN_POINT('Ctrl Pts',(-20.8944820635889,11.1525008815456,
2.00467516608211));
#128816=CARTESIAN_POINT('Ctrl Pts',(-20.8880136068027,11.0165581255621,
1.97683522296837));
#128817=CARTESIAN_POINT('Ctrl Pts',(-20.8815451500165,10.8794355313552,
1.95454015043084));
#128818=CARTESIAN_POINT('Ctrl Pts',(-20.8750766932303,10.7416323549925,
1.93787643572666));
#128819=CARTESIAN_POINT('Ctrl Pts',(-20.868608190712,10.6038282043591,1.92121260320976));
#128820=CARTESIAN_POINT('Ctrl Pts',(-20.8621396881937,10.4653438603421,
1.91018025615929));
#128821=CARTESIAN_POINT('Ctrl Pts',(-20.8556711856754,10.3266848256182,
1.90481412070709));
#128822=CARTESIAN_POINT('Ctrl Pts',(-20.8492011591068,10.1879931213016,
1.89944672093439));
#128823=CARTESIAN_POINT('Ctrl Pts',(-20.8427311325382,10.0491270452858,
1.89974820296182));
#128824=CARTESIAN_POINT('Ctrl Pts',(-20.8362611059696,9.91059269124868,
1.90570116795498));
#128825=CARTESIAN_POINT('Ctrl Pts',(-20.8297838192034,9.77190288394011,
1.91166081293658));
#128826=CARTESIAN_POINT('Ctrl Pts',(-20.8233065324371,9.6335459434392,1.92328458861965));
#128827=CARTESIAN_POINT('Ctrl Pts',(-20.8168292456708,9.49602388099488,
1.94050308759357));
#128828=CARTESIAN_POINT('Ctrl Pts',(-20.8103483111699,9.35842437192744,
1.95773128329961));
#128829=CARTESIAN_POINT('Ctrl Pts',(-20.803867376669,9.22166107196966,1.98056040833072));
#128830=CARTESIAN_POINT('Ctrl Pts',(-20.7973864421682,9.08622511032575,
2.00887001726311));
#128831=CARTESIAN_POINT('Ctrl Pts',(-20.7908944963577,8.95055903876371,
2.03722772510301));
#128832=CARTESIAN_POINT('Ctrl Pts',(-20.7844025505471,8.81622519909787,
2.07108441947432));
#128833=CARTESIAN_POINT('Ctrl Pts',(-20.7779106047366,8.68369966808103,
2.1102697006662));
#128834=CARTESIAN_POINT('Ctrl Pts',(-20.7716026590288,8.55493028537777,
2.14834436017835));
#128835=CARTESIAN_POINT('Ctrl Pts',(-20.7652947133209,8.42786837597987,
2.19144945063097));
#128836=CARTESIAN_POINT('Ctrl Pts',(-20.758986767613,8.30292988577589,2.23938631919967));
#128837=CARTESIAN_POINT('Ctrl Pts',(-20.7522553481606,8.16960385187237,
2.29054135199688));
#128838=CARTESIAN_POINT('Ctrl Pts',(-20.7455239287083,8.0382566326181,2.34736719785055));
#128839=CARTESIAN_POINT('Ctrl Pts',(-20.7387925092559,7.90939433831116,
2.4096915298711));
#128840=CARTESIAN_POINT('Ctrl Pts',(-20.7320693374223,7.7806899315173,2.47193949949378));
#128841=CARTESIAN_POINT('Ctrl Pts',(-20.7253461655886,7.65446471705759,
2.53967237964706));
#128842=CARTESIAN_POINT('Ctrl Pts',(-20.718622993755,7.53120645650351,2.6126691870997));
#128843=CARTESIAN_POINT('Ctrl Pts',(-20.7119066869372,7.40807405468524,
2.68559145767453));
#128844=CARTESIAN_POINT('Ctrl Pts',(-20.7051903801194,7.28790288938902,
2.76376676295887));
#128845=CARTESIAN_POINT('Ctrl Pts',(-20.6984740733016,7.17115757741741,
2.8469275095722));
#128846=CARTESIAN_POINT('Ctrl Pts',(-20.691763254633,7.05450766246991,2.93002030238408));
#128847=CARTESIAN_POINT('Ctrl Pts',(-20.6850524359643,6.94127832456694,
3.0180902078119));
#128848=CARTESIAN_POINT('Ctrl Pts',(-20.6783416172957,6.83190647329252,
3.11082554613232));
#128849=CARTESIAN_POINT('Ctrl Pts',(-20.6716350376826,6.72260370946926,
3.20350230586892));
#128850=CARTESIAN_POINT('Ctrl Pts',(-20.6649284580695,6.6171538582951,3.30083838763056));
#128851=CARTESIAN_POINT('Ctrl Pts',(-20.6582218784564,6.51596181868043,
3.40248101990474));
#128852=CARTESIAN_POINT('Ctrl Pts',(-20.651517616954,6.41480475581314,3.50408851968543));
#128853=CARTESIAN_POINT('Ctrl Pts',(-20.6448133554515,6.31790283410827,
3.60999934380801));
#128854=CARTESIAN_POINT('Ctrl Pts',(-20.638109093949,6.22562508005278,3.7198229301748));
#128855=CARTESIAN_POINT('Ctrl Pts',(-20.6314059106226,6.13336216605965,
3.82962885476722));
#128856=CARTESIAN_POINT('Ctrl Pts',(-20.6247027272961,6.04572217583957,
3.94334600500746));
#128857=CARTESIAN_POINT('Ctrl Pts',(-20.6179995439696,5.96303463779049,
4.06054981578045));
#128858=CARTESIAN_POINT('Ctrl Pts',(-20.6112961998865,5.88034511671715,
4.17775643735183));
#128859=CARTESIAN_POINT('Ctrl Pts',(-20.6045928558033,5.80260849649827,
4.29844958329638));
#128860=CARTESIAN_POINT('Ctrl Pts',(-20.5978895117201,5.73011159094298,
4.4221748262819));
#128861=CARTESIAN_POINT('Ctrl Pts',(-20.5911822561601,5.65757238262621,
4.54597226434116));
#128862=CARTESIAN_POINT('Ctrl Pts',(-20.5844750006002,5.5902791850645,4.67280501527352));
#128863=CARTESIAN_POINT('Ctrl Pts',(-20.5777677450402,5.52847358717437,
4.80219269532544));
#128864=CARTESIAN_POINT('Ctrl Pts',(-20.5710584023763,5.46664875716989,
4.93162063708084));
#128865=CARTESIAN_POINT('Ctrl Pts',(-20.5643490597123,5.41031508149065,
5.06360475507181));
#128866=CARTESIAN_POINT('Ctrl Pts',(-20.5576397170484,5.35966624389706,
5.19764405869958));
#128867=CARTESIAN_POINT('Ctrl Pts',(-20.550923952482,5.3089689273521,5.33181165914898));
#128868=CARTESIAN_POINT('Ctrl Pts',(-20.5442081879156,5.26396744082792,
5.4680380257195));
#128869=CARTESIAN_POINT('Ctrl Pts',(-20.5374924233492,5.22480597472622,
5.60580578166324));
#128870=CARTESIAN_POINT('Ctrl Pts',(-20.533760108165,5.20304182067926,5.68237080747907));
#128871=CARTESIAN_POINT('Ctrl Pts',(-20.5300277929808,5.18308053177186,
5.75941167581817));
#128872=CARTESIAN_POINT('Ctrl Pts',(-20.5262954777966,5.16494003467883,
5.83683820956401));
#128873=CARTESIAN_POINT('Ctrl Pts',(-20.5195533162237,5.13217051860648,
5.97670372862885));
#128874=CARTESIAN_POINT('Ctrl Pts',(-20.5128111546507,5.10528904643071,
6.11806934857141));
#128875=CARTESIAN_POINT('Ctrl Pts',(-20.5060689930777,5.08442238336994,
6.26041035554957));
#128876=CARTESIAN_POINT('Ctrl Pts',(-20.4993317332857,5.06357089108352,
6.40264787577027));
#128877=CARTESIAN_POINT('Ctrl Pts',(-20.4925944734937,5.04872555025024,
6.54585900974906));
#128878=CARTESIAN_POINT('Ctrl Pts',(-20.4858572137017,5.03996208500972,
6.68950875716634));
#128879=CARTESIAN_POINT('Ctrl Pts',(-20.4791236997967,5.03120349221757,
6.83307863595198));
#128880=CARTESIAN_POINT('Ctrl Pts',(-20.4723901858916,5.02852005962299,
6.9770862778926));
#128881=CARTESIAN_POINT('Ctrl Pts',(-20.4656566719866,5.03193567501757,
7.12099153964812));
#128882=CARTESIAN_POINT('Ctrl Pts',(-20.4589254983211,5.0353501033116,7.26484678698583));
#128883=CARTESIAN_POINT('Ctrl Pts',(-20.4521943246556,5.04485934699362,
7.40859935977437));
#128884=CARTESIAN_POINT('Ctrl Pts',(-20.4454631509901,5.06043518884772,
7.55170910844189));
#128885=CARTESIAN_POINT('Ctrl Pts',(-20.4387320860167,5.07601077918977,
7.69481654623414));
#128886=CARTESIAN_POINT('Ctrl Pts',(-20.4320010210433,5.09765273928883,
7.83728081633733));
#128887=CARTESIAN_POINT('Ctrl Pts',(-20.4252699560699,5.12528095940224,
7.97856670376571));
#128888=CARTESIAN_POINT('Ctrl Pts',(-20.4201632483428,5.14624186910957,
8.08575713142076));
#128889=CARTESIAN_POINT('Ctrl Pts',(-20.4150565406156,5.17064735025746,
8.19226935385378));
#128890=CARTESIAN_POINT('Ctrl Pts',(-20.4099498328884,5.19844276440152,
8.29787346812079));
#128891=CARTESIAN_POINT('Ctrl Pts',(-20.4026901610334,5.23795659533554,
8.44799978375887));
#128892=CARTESIAN_POINT('Ctrl Pts',(-20.3954304891783,5.28430814356502,
8.59623550876125));
#128893=CARTESIAN_POINT('Ctrl Pts',(-20.3881708173233,5.33728986957224,
8.74198825077139));
#128894=CARTESIAN_POINT('Ctrl Pts',(-20.3809013580099,5.39034302531422,
8.88793749600039));
#128895=CARTESIAN_POINT('Ctrl Pts',(-20.3736318986965,5.45004414095369,
9.03139682741447));
#128896=CARTESIAN_POINT('Ctrl Pts',(-20.3663624393832,5.51613698008329,
9.17179249618029));
#128897=CARTESIAN_POINT('Ctrl Pts',(-20.3617627351688,5.55795680430693,
9.26062696398146));
#128898=CARTESIAN_POINT('Ctrl Pts',(-20.3571630309544,5.60233469474515,
9.34823528301885));
#128899=CARTESIAN_POINT('Ctrl Pts',(-20.35256332674,5.6491961756188,9.4344770775744));
#128900=CARTESIAN_POINT('Ctrl Pts',(-21.8525208770954,5.64940737302611,
9.43436256508443));
#128901=CARTESIAN_POINT('Ctrl Pts',(-21.8370464419925,5.80706920978094,
9.7249012359362));
#128902=CARTESIAN_POINT('Ctrl Pts',(-21.7827901252536,6.45799744036311,
10.6901681088921));
#128903=CARTESIAN_POINT('Ctrl Pts',(-21.6973986661372,7.9715431412064,11.8045112188381));
#128904=CARTESIAN_POINT('Ctrl Pts',(-21.6274816421238,9.46413915462446,
12.0984964029847));
#128905=CARTESIAN_POINT('Ctrl Pts',(-21.5963464997463,10.1291160878984,
12.0991317151048));
#128906=CARTESIAN_POINT('',(-21.7216535043236,10.1295436686122,12.098999999813));
#128907=CARTESIAN_POINT('Ctrl Pts',(-21.9778242975584,5.64919617561881,
9.43447707757441));
#128908=CARTESIAN_POINT('Ctrl Pts',(-21.9708911970379,5.71990566836338,
9.56460769727989));
#128909=CARTESIAN_POINT('Ctrl Pts',(-21.9639580965173,5.79629143323561,
9.69166108851864));
#128910=CARTESIAN_POINT('Ctrl Pts',(-21.9570249959968,5.87805954066539,
9.81514742433371));
#128911=CARTESIAN_POINT('Ctrl Pts',(-21.9500922126906,5.95982390690941,
9.93862811020363));
#128912=CARTESIAN_POINT('Ctrl Pts',(-21.9431594293844,6.04696993941788,
10.0585417924252));
#128913=CARTESIAN_POINT('Ctrl Pts',(-21.9362266460782,6.13916035711196,
10.1744275916134));
#128914=CARTESIAN_POINT('Ctrl Pts',(-21.9292923813661,6.2313704741715,10.2903381534262));
#128915=CARTESIAN_POINT('Ctrl Pts',(-21.922358116654,6.32862692396764,10.4022188541319));
#128916=CARTESIAN_POINT('Ctrl Pts',(-21.9154238519419,6.43055173913713,
10.5096414009781));
#128917=CARTESIAN_POINT('Ctrl Pts',(-21.912002891723,6.48083547540742,10.5626373961743));
#128918=CARTESIAN_POINT('Ctrl Pts',(-21.9085819315041,6.53225482388749,
10.6145488689097));
#128919=CARTESIAN_POINT('Ctrl Pts',(-21.9051609712852,6.58476102287579,
10.6653276230177));
#128920=CARTESIAN_POINT('Ctrl Pts',(-21.8982288574645,6.69115774320861,
10.7682239096234));
#128921=CARTESIAN_POINT('Ctrl Pts',(-21.8912967436438,6.80205628720019,
10.8665022681371));
#128922=CARTESIAN_POINT('Ctrl Pts',(-21.8843646298231,6.91703324183498,
10.959780085773));
#128923=CARTESIAN_POINT('Ctrl Pts',(-21.8774338365917,7.03198829300128,
11.0530401336938));
#128924=CARTESIAN_POINT('Ctrl Pts',(-21.8705030433603,7.15101994789284,
11.1413013330035));
#128925=CARTESIAN_POINT('Ctrl Pts',(-21.8635722501289,7.27367163221511,
11.224221269507));
#128926=CARTESIAN_POINT('Ctrl Pts',(-21.8566412042781,7.39632778705101,
11.3071442283473));
#128927=CARTESIAN_POINT('Ctrl Pts',(-21.8497101584272,7.5226039631228,11.3847253467467));
#128928=CARTESIAN_POINT('Ctrl Pts',(-21.8427791125763,7.65201406730425,
11.456665171773));
#128929=CARTESIAN_POINT('Ctrl Pts',(-21.8358484336565,7.78141732048731,
11.5286011882897));
#128930=CARTESIAN_POINT('Ctrl Pts',(-21.8289177547366,7.91395388012152,
11.5948963491392));
#128931=CARTESIAN_POINT('Ctrl Pts',(-21.8219870758168,8.04911248293117,
11.6552968518478));
#128932=CARTESIAN_POINT('Ctrl Pts',(-21.815054830091,8.18430164079941,11.7157110091879));
#128933=CARTESIAN_POINT('Ctrl Pts',(-21.8081225843652,8.32211372406546,
11.7702277106697));
#128934=CARTESIAN_POINT('Ctrl Pts',(-21.8011903386395,8.46201631468178,
11.8186407999764));
#128935=CARTESIAN_POINT('Ctrl Pts',(-21.797065334552,8.54526477138265,11.8474488081138));
#128936=CARTESIAN_POINT('Ctrl Pts',(-21.7929403304645,8.62925305861431,
11.8740965742915));
#128937=CARTESIAN_POINT('Ctrl Pts',(-21.788815326377,8.71386618713863,11.898548959425));
#128938=CARTESIAN_POINT('Ctrl Pts',(-21.7818417513357,8.85690992448683,
11.939887231837));
#128939=CARTESIAN_POINT('Ctrl Pts',(-21.7748681762943,9.00178738562049,
11.9749620552806));
#128940=CARTESIAN_POINT('Ctrl Pts',(-21.7678946012529,9.14793866626696,
12.0036325152953));
#128941=CARTESIAN_POINT('Ctrl Pts',(-21.7609225553009,9.29405790045778,
12.0322966887649));
#128942=CARTESIAN_POINT('Ctrl Pts',(-21.7539505093488,9.44145008039454,
12.0545592393556));
#128943=CARTESIAN_POINT('Ctrl Pts',(-21.7469784633968,9.58954487878361,
12.0703303114365));
#128944=CARTESIAN_POINT('Ctrl Pts',(-21.740007262077,9.73762173614916,12.0860994729225));
#128945=CARTESIAN_POINT('Ctrl Pts',(-21.7330360607571,9.88640072158192,
12.0953786905622));
#128946=CARTESIAN_POINT('Ctrl Pts',(-21.7260648594373,10.0353056921974,
12.0981298955968));
#128947=CARTESIAN_POINT('Ctrl Pts',(-21.7245944077477,10.0667145635801,
12.0987102136662));
#128948=CARTESIAN_POINT('Ctrl Pts',(-21.723123956058,10.0981290288572,12.0990002688469));
#128949=CARTESIAN_POINT('Ctrl Pts',(-21.7216535043684,10.1295436676547,
12.098999999813));
#128950=CARTESIAN_POINT('Ctrl Pts',(-21.7216535043236,10.1295436686122,
12.098999999813));
#128951=CARTESIAN_POINT('Ctrl Pts',(-21.7145780772905,10.2807026533976,
12.0989987052645));
#128952=CARTESIAN_POINT('Ctrl Pts',(-21.7075026502575,10.4318398568485,
12.0922714484638));
#128953=CARTESIAN_POINT('Ctrl Pts',(-21.7004272232244,10.582361479932,12.0788500155049));
#128954=CARTESIAN_POINT('Ctrl Pts',(-21.693349719895,10.7329272738466,12.0654246440032));
#128955=CARTESIAN_POINT('Ctrl Pts',(-21.6862722165656,10.8828768275428,
12.0453011997449));
#128956=CARTESIAN_POINT('Ctrl Pts',(-21.6791947132363,11.0316213327613,
12.0185633503003));
#128957=CARTESIAN_POINT('Ctrl Pts',(-21.6769530359805,11.0787335923755,
12.0100945971002));
#128958=CARTESIAN_POINT('Ctrl Pts',(-21.6747113587247,11.1257250216099,
12.0009626767532));
#128959=CARTESIAN_POINT('Ctrl Pts',(-21.6724696814689,11.1725771008058,
11.9911713216213));
#128960=CARTESIAN_POINT('Ctrl Pts',(-21.665538500834,11.3174419439415,11.9608968247447));
#128961=CARTESIAN_POINT('Ctrl Pts',(-21.6586073201992,11.4610130681156,
11.9243059246399));
#128962=CARTESIAN_POINT('Ctrl Pts',(-21.6516761395644,11.6027362745548,
11.88153417271));
#128963=CARTESIAN_POINT('Ctrl Pts',(-21.6447462728878,11.7444326142333,
11.8387705291094));
#128964=CARTESIAN_POINT('Ctrl Pts',(-21.6378164062113,11.884281418354,11.7898284670043));
#128965=CARTESIAN_POINT('Ctrl Pts',(-21.6308865395347,12.0217431373186,
11.7348935478288));
#128966=CARTESIAN_POINT('Ctrl Pts',(-21.6239564014542,12.1592102398846,
11.6799564771618));
#128967=CARTESIAN_POINT('Ctrl Pts',(-21.6170262633738,12.2942897616118,
11.6190261995686));
#128968=CARTESIAN_POINT('Ctrl Pts',(-21.6100961252933,12.426461132908,11.5523368234249));
#128969=CARTESIAN_POINT('Ctrl Pts',(-21.6031663413856,12.5586257494336,
11.4856508555187));
#128970=CARTESIAN_POINT('Ctrl Pts',(-21.5962365574778,12.6878822178597,
11.4132065281025));
#128971=CARTESIAN_POINT('Ctrl Pts',(-21.5893067735701,12.8137336190688,
11.3352844056949));
#128972=CARTESIAN_POINT('Ctrl Pts',(-21.5823753954677,12.9396139723548,
11.2573443573264));
#128973=CARTESIAN_POINT('Ctrl Pts',(-21.5754440173652,13.0620874116896,
11.1739241703709));
#128974=CARTESIAN_POINT('Ctrl Pts',(-21.5685126392628,13.1806845732687,
11.0853486631923));
#128975=CARTESIAN_POINT('Ctrl Pts',(-21.5643831050287,13.2513416679423,
11.0325776869467));
#128976=CARTESIAN_POINT('Ctrl Pts',(-21.5602535707947,13.3206234444385,
10.9779776769825));
#128977=CARTESIAN_POINT('Ctrl Pts',(-21.5561240365606,13.3884359580966,
10.9216243345105));
#128978=CARTESIAN_POINT('Ctrl Pts',(-21.5491919873467,13.5022695420679,
10.8270267064872));
#128979=CARTESIAN_POINT('Ctrl Pts',(-21.5422599381329,13.6120015769791,
10.7274526569437));
#128980=CARTESIAN_POINT('Ctrl Pts',(-21.535327888919,13.7172057131023,10.6232814845348));
#128981=CARTESIAN_POINT('Ctrl Pts',(-21.5283971834842,13.8223894553827,
10.5191305057286));
#128982=CARTESIAN_POINT('Ctrl Pts',(-21.5214664780495,13.9230468150587,
10.4103844146959));
#128983=CARTESIAN_POINT('Ctrl Pts',(-21.5145357726147,14.0187877971565,
10.2974598452277));
#128984=CARTESIAN_POINT('Ctrl Pts',(-21.5076048482097,14.1145318041177,
10.1845317079939));
#128985=CARTESIAN_POINT('Ctrl Pts',(-21.5006739238046,14.2053589060595,
10.06742507829));
#128986=CARTESIAN_POINT('Ctrl Pts',(-21.4937429993995,14.2909186070078,
9.94659060224677));
#128987=CARTESIAN_POINT('Ctrl Pts',(-21.4868124606186,14.3764735475678,
9.82576284921712));
#128988=CARTESIAN_POINT('Ctrl Pts',(-21.4798819218377,14.4567614830456,
9.70120793542299));
#128989=CARTESIAN_POINT('Ctrl Pts',(-21.4729513830568,14.5314745604009,
9.57340649132294));
#128990=CARTESIAN_POINT('Ctrl Pts',(-21.4660193048808,14.6062042328509,
9.44557666026405));
#128991=CARTESIAN_POINT('Ctrl Pts',(-21.4590872267048,14.6753564058714,
9.31449914377409));
#128992=CARTESIAN_POINT('Ctrl Pts',(-21.4521551485288,14.7386682911608,
9.18068077988451));
#128993=CARTESIAN_POINT('Ctrl Pts',(-21.4480295629033,14.7763479879615,
9.10103956631653));
#128994=CARTESIAN_POINT('Ctrl Pts',(-21.4439039772779,14.8119599512988,
9.020428027734));
#128995=CARTESIAN_POINT('Ctrl Pts',(-21.4397783916524,14.8454567318764,
8.93895670479501));
#128996=CARTESIAN_POINT('Ctrl Pts',(-21.4328287564197,14.9018827590196,
8.80171655812195));
#128997=CARTESIAN_POINT('Ctrl Pts',(-21.425879121187,14.9523225305843,8.661990870534));
#128998=CARTESIAN_POINT('Ctrl Pts',(-21.4189294859543,14.9965767489365,
8.52031737474841));
#128999=CARTESIAN_POINT('Ctrl Pts',(-21.4119810766083,15.0408231610291,
8.37866886957668));
#129000=CARTESIAN_POINT('Ctrl Pts',(-21.4050326672623,15.0788860995113,
8.23507355414718));
#129001=CARTESIAN_POINT('Ctrl Pts',(-21.3980842579163,15.110615897284,8.09008505072978));
#129002=CARTESIAN_POINT('Ctrl Pts',(-21.3911356289697,15.1423466978592,
7.94509196503175));
#129003=CARTESIAN_POINT('Ctrl Pts',(-21.3841870000231,15.1677438841323,
7.79870592238976));
#129004=CARTESIAN_POINT('Ctrl Pts',(-21.3772383710765,15.1867086284737,
7.65149204760402));
#129005=CARTESIAN_POINT('Ctrl Pts',(-21.3702901717336,15.2056722003069,
7.50428727441542));
#129006=CARTESIAN_POINT('Ctrl Pts',(-21.3633419723906,15.2182040846995,
7.35625509628934));
#129007=CARTESIAN_POINT('Ctrl Pts',(-21.3563937730477,15.2242571742947,
7.20796714878315));
#129008=CARTESIAN_POINT('Ctrl Pts',(-21.349444258653,15.2303114095286,7.05965113554095));
#129009=CARTESIAN_POINT('Ctrl Pts',(-21.3424947442583,15.2298843862783,
6.91107958341258));
#129010=CARTESIAN_POINT('Ctrl Pts',(-21.3355452298636,15.2229810863828,
6.76282617627361));
#129011=CARTESIAN_POINT('Ctrl Pts',(-21.3315077354905,15.2189704414799,
6.67669464777756));
#129012=CARTESIAN_POINT('Ctrl Pts',(-21.3274702411173,15.2127748193448,
6.59067051003166));
#129013=CARTESIAN_POINT('Ctrl Pts',(-21.3234327467442,15.204403268655,6.50486586282613));
#129014=CARTESIAN_POINT('Ctrl Pts',(-21.3165507415352,15.190133761349,6.35860980041301));
#129015=CARTESIAN_POINT('Ctrl Pts',(-21.3096687363261,15.1695340759322,
6.21293699097909));
#129016=CARTESIAN_POINT('Ctrl Pts',(-21.3027867311171,15.1426759370888,
6.06840565491517));
#129017=CARTESIAN_POINT('Ctrl Pts',(-21.2959062311046,15.1158236725187,
5.92390592999826));
#129018=CARTESIAN_POINT('Ctrl Pts',(-21.2890257310922,15.0827157467963,
5.78054751496051));
#129019=CARTESIAN_POINT('Ctrl Pts',(-21.2821452310798,15.0434752182249,
5.6388796692902));
#129020=CARTESIAN_POINT('Ctrl Pts',(-21.2752642995611,15.0042322287083,
5.49720293900931));
#129021=CARTESIAN_POINT('Ctrl Pts',(-21.2683833680424,14.9588559542225,
5.35721731924814));
#129022=CARTESIAN_POINT('Ctrl Pts',(-21.2615024365237,14.9075198065232,
5.21945858557805));
#129023=CARTESIAN_POINT('Ctrl Pts',(-21.2546216674167,14.8561848705187,
5.0817031034479));
#129024=CARTESIAN_POINT('Ctrl Pts',(-21.2477408983096,14.7988904640696,
4.94617472034536));
#129025=CARTESIAN_POINT('Ctrl Pts',(-21.2408601292026,14.7358587467216,
4.81339073071985));
#129026=CARTESIAN_POINT('Ctrl Pts',(-21.2339770585297,14.6728059457358,
4.68056232584361));
#129027=CARTESIAN_POINT('Ctrl Pts',(-21.2270939878569,14.6040121460501,
4.5504804560362));
#129028=CARTESIAN_POINT('Ctrl Pts',(-21.2202109171841,14.5297464825698,
4.42363979757638));
#129029=CARTESIAN_POINT('Ctrl Pts',(-21.2158363120681,14.4825461897283,
4.3430249354323));
#129030=CARTESIAN_POINT('Ctrl Pts',(-21.2114617069521,14.4331365440049,
4.26371883720866));
#129031=CARTESIAN_POINT('Ctrl Pts',(-21.2070871018361,14.3815959889042,
4.1858428080249));
#129032=CARTESIAN_POINT('Ctrl Pts',(-21.2000237327386,14.2983770572496,
4.0601018272089));
#129033=CARTESIAN_POINT('Ctrl Pts',(-21.1929603636411,14.2095738290717,
3.93804985679066));
#129034=CARTESIAN_POINT('Ctrl Pts',(-21.1858969945437,14.1155331325974,
3.82016653488964));
#129035=CARTESIAN_POINT('Ctrl Pts',(-21.178834458356,14.0215035253657,3.70229711374445));
#129036=CARTESIAN_POINT('Ctrl Pts',(-21.1717719221683,13.9222378725607,
3.58859559695674));
#129037=CARTESIAN_POINT('Ctrl Pts',(-21.1647093859805,13.8181238245223,
3.47950922722885));
#129038=CARTESIAN_POINT('Ctrl Pts',(-21.1576473847886,13.7140176632508,
3.37043112092746));
#129039=CARTESIAN_POINT('Ctrl Pts',(-21.1505853835967,13.6050640485619,
3.26596768458527));
#129040=CARTESIAN_POINT('Ctrl Pts',(-21.1435233824048,13.4916885213516,
3.16653037746596));
#129041=CARTESIAN_POINT('Ctrl Pts',(-21.1364626336035,13.3783331004038,
3.06711070477482));
#129042=CARTESIAN_POINT('Ctrl Pts',(-21.1294018848022,13.2605575614681,
2.97271558142976));
#129043=CARTESIAN_POINT('Ctrl Pts',(-21.1223411360009,13.1388219318202,
2.88371739178833));
#129044=CARTESIAN_POINT('Ctrl Pts',(-21.1152814326218,13.0171043264813,
2.79473237931509));
#129045=CARTESIAN_POINT('Ctrl Pts',(-21.1082217292426,12.8914280458127,
2.71114288504483));
#129046=CARTESIAN_POINT('Ctrl Pts',(-21.1011620258634,12.7622840994283,
2.63327939000014));
#129047=CARTESIAN_POINT('Ctrl Pts',(-21.0976885028849,12.6987425536711,
2.59496890800147));
#129048=CARTESIAN_POINT('Ctrl Pts',(-21.0942149799064,12.6343619930903,
2.55804394760152));
#129049=CARTESIAN_POINT('Ctrl Pts',(-21.0907414569279,12.5692033929549,
2.52253996618568));
#129050=CARTESIAN_POINT('Ctrl Pts',(-21.0840199577374,12.4431171454252,
2.4538373884787));
#129051=CARTESIAN_POINT('Ctrl Pts',(-21.0772984585468,12.3140777046371,
2.39043779766263));
#129052=CARTESIAN_POINT('Ctrl Pts',(-21.0705769593563,12.1825638082227,
2.33258851188734));
#129053=CARTESIAN_POINT('Ctrl Pts',(-21.0638571099993,12.0510821927081,
2.27475342557727));
#129054=CARTESIAN_POINT('Ctrl Pts',(-21.0571372606424,11.917127668362,2.2224660775447));
#129055=CARTESIAN_POINT('Ctrl Pts',(-21.0504174112854,11.7812007609424,
2.17592645202188));
#129056=CARTESIAN_POINT('Ctrl Pts',(-21.0436962436786,11.6452471883979,
2.12937769670309));
#129057=CARTESIAN_POINT('Ctrl Pts',(-21.0369750760718,11.5073208059466,
2.08857904163403));
#129058=CARTESIAN_POINT('Ctrl Pts',(-21.030253908465,11.3679394888552,2.05368130500632));
#129059=CARTESIAN_POINT('Ctrl Pts',(-21.0235322550113,11.2285480964327,
2.01878104575749));
#129060=CARTESIAN_POINT('Ctrl Pts',(-21.0168106015575,11.0877019181293,
1.98978263908414));
#129061=CARTESIAN_POINT('Ctrl Pts',(-21.0100889481037,10.9459306945815,
1.96678612406097));
#129062=CARTESIAN_POINT('Ctrl Pts',(-21.00336283355,10.8040653787673,1.94377434646079));
#129063=CARTESIAN_POINT('Ctrl Pts',(-20.9966367189962,10.6612741552295,
1.92677247459323));
#129064=CARTESIAN_POINT('Ctrl Pts',(-20.9899106044424,10.5180941451528,
1.91582891806806));
#129065=CARTESIAN_POINT('Ctrl Pts',(-20.9847390069682,10.4080054197001,
1.90741459969269));
#129066=CARTESIAN_POINT('Ctrl Pts',(-20.9795674094939,10.2976870254571,
1.90258079609333));
#129067=CARTESIAN_POINT('Ctrl Pts',(-20.9743958120197,10.1873835904047,
1.90132855638237));
#129068=CARTESIAN_POINT('Ctrl Pts',(-20.9671170684873,10.0321374757399,
1.89956609676666));
#129069=CARTESIAN_POINT('Ctrl Pts',(-20.959838324955,9.87682543926592,1.90489862489669));
#129070=CARTESIAN_POINT('Ctrl Pts',(-20.9525595814226,9.7220753784726,1.91730325734721));
#129071=CARTESIAN_POINT('Ctrl Pts',(-20.9452817167969,9.56734400371569,
1.92970639194104));
#129072=CARTESIAN_POINT('Ctrl Pts',(-20.9380038521713,9.41317472155407,
1.94917990409636));
#129073=CARTESIAN_POINT('Ctrl Pts',(-20.9307259875456,9.26019127590926,
1.97564896307795));
#129074=CARTESIAN_POINT('Ctrl Pts',(-20.9234524716548,9.10729924230271,
2.00210220603041));
#129075=CARTESIAN_POINT('Ctrl Pts',(-20.9161789557639,8.95559187901386,
2.03554260156708));
#129076=CARTESIAN_POINT('Ctrl Pts',(-20.9089054398731,8.80568411965762,
2.07584397942619));
#129077=CARTESIAN_POINT('Ctrl Pts',(-20.9016367742746,8.65587632522299,
2.11611848259851));
#129078=CARTESIAN_POINT('Ctrl Pts',(-20.894368108676,8.50786598368629,2.16324476993341));
#129079=CARTESIAN_POINT('Ctrl Pts',(-20.8870994430774,8.36225537649466,
2.21704615946469));
#129080=CARTESIAN_POINT('Ctrl Pts',(-20.8798397779555,8.21682507266881,
2.27078092904428));
#129081=CARTESIAN_POINT('Ctrl Pts',(-20.8725801128336,8.07378880792323,
2.33117421095855));
#129082=CARTESIAN_POINT('Ctrl Pts',(-20.8653204477117,7.93373154482647,
2.39800022911074));
#129083=CARTESIAN_POINT('Ctrl Pts',(-20.862897020845,7.88697752400415,2.42030814071116));
#129084=CARTESIAN_POINT('Ctrl Pts',(-20.8604735939782,7.84055533141693,
2.44333248635513));
#129085=CARTESIAN_POINT('Ctrl Pts',(-20.8580501671115,7.79448628016983,
2.46706365275169));
#129086=CARTESIAN_POINT('Ctrl Pts',(-20.8513195102469,7.6665373082926,2.53297294021673));
#129087=CARTESIAN_POINT('Ctrl Pts',(-20.8445888533824,7.54135727855362,
2.6043155917558));
#129088=CARTESIAN_POINT('Ctrl Pts',(-20.8378581965178,7.41941799831926,
2.68082686800284));
#129089=CARTESIAN_POINT('Ctrl Pts',(-20.8311277589209,7.29748269055658,
2.75733565170707));
#129090=CARTESIAN_POINT('Ctrl Pts',(-20.824397321324,7.17878823114962,2.83901252941112));
#129091=CARTESIAN_POINT('Ctrl Pts',(-20.8176668837272,7.06377874695439,
2.92554860151401));
#129092=CARTESIAN_POINT('Ctrl Pts',(-20.8109330039709,6.94871044325873,
3.01212893091069));
#129093=CARTESIAN_POINT('Ctrl Pts',(-20.8041991242146,6.83733117429048,
3.10357320184736));
#129094=CARTESIAN_POINT('Ctrl Pts',(-20.7974652444583,6.73005358099377,
3.19953094417206));
#129095=CARTESIAN_POINT('Ctrl Pts',(-20.7907296988947,6.62274944968287,
3.29551242423964));
#129096=CARTESIAN_POINT('Ctrl Pts',(-20.7839941533312,6.51954928410615,
3.3960093515451));
#129097=CARTESIAN_POINT('Ctrl Pts',(-20.7772586077676,6.42082972916417,
3.50063351130258));
#129098=CARTESIAN_POINT('Ctrl Pts',(-20.7705168109826,6.32201855316575,
3.60535477214659));
#129099=CARTESIAN_POINT('Ctrl Pts',(-20.7637750141976,6.22769654299804,
3.7142106479578));
#129100=CARTESIAN_POINT('Ctrl Pts',(-20.7570332174125,6.13820130284807,
3.82677833895687));
#129101=CARTESIAN_POINT('Ctrl Pts',(-20.7519236523428,6.07037342734832,
3.91209267877634));
#129102=CARTESIAN_POINT('Ctrl Pts',(-20.746814087273,6.00531726134624,3.99953837678175));
#129103=CARTESIAN_POINT('Ctrl Pts',(-20.7417045222033,5.9431632940884,4.08892013425649));
#129104=CARTESIAN_POINT('Ctrl Pts',(-20.7349885840485,5.86146902178138,
4.20640221877302));
#129105=CARTESIAN_POINT('Ctrl Pts',(-20.7282726458937,5.7846499298272,4.32743176090146));
#129106=CARTESIAN_POINT('Ctrl Pts',(-20.7215567077389,5.7130174542218,4.45157246074438));
#129107=CARTESIAN_POINT('Ctrl Pts',(-20.7148461284493,5.64144213649507,
4.5756141046912));
#129108=CARTESIAN_POINT('Ctrl Pts',(-20.7081355491596,5.57504537611946,
4.70276164277715));
#129109=CARTESIAN_POINT('Ctrl Pts',(-20.70142496987,5.51409512437855,4.83255015419278));
#129110=CARTESIAN_POINT('Ctrl Pts',(-20.6947183775871,5.45318108546702,
4.96226155338845));
#129111=CARTESIAN_POINT('Ctrl Pts',(-20.6880117853042,5.39770726562995,
5.09461046626503));
#129112=CARTESIAN_POINT('Ctrl Pts',(-20.6813051930213,5.34789546567042,
5.22910783013794));
#129113=CARTESIAN_POINT('Ctrl Pts',(-20.6746012193564,5.2981031149441,5.36355267893212));
#129114=CARTESIAN_POINT('Ctrl Pts',(-20.6678972456915,5.25396850735589,
5.50014396102872));
#129115=CARTESIAN_POINT('Ctrl Pts',(-20.6611932720266,5.2156650969859,5.63837319873601));
#129116=CARTESIAN_POINT('Ctrl Pts',(-20.6544892305015,5.17736129889393,
5.77660383565325));
#129117=CARTESIAN_POINT('Ctrl Pts',(-20.6477851889764,5.14488892341421,
5.91647210752774));
#129118=CARTESIAN_POINT('Ctrl Pts',(-20.6410811474513,5.11837144179926,
6.05745473679778));
#129119=CARTESIAN_POINT('Ctrl Pts',(-20.6343767553807,5.0918525736203,6.1984447378628));
#129120=CARTESIAN_POINT('Ctrl Pts',(-20.6276723633102,5.07128928850254,
6.34054884896834));
#129121=CARTESIAN_POINT('Ctrl Pts',(-20.6209679712396,5.05675377886092,
6.48323431236274));
#129122=CARTESIAN_POINT('Ctrl Pts',(-20.6142619894755,5.04221482267187,
6.62595360822882));
#129123=CARTESIAN_POINT('Ctrl Pts',(-20.6075560077115,5.03370652666762,
6.76925416302977));
#129124=CARTESIAN_POINT('Ctrl Pts',(-20.6008500259474,5.03124911809654,
6.91259894067805));
#129125=CARTESIAN_POINT('Ctrl Pts',(-20.5941412144946,5.02879067258536,
7.05600420478712));
#129126=CARTESIAN_POINT('Ctrl Pts',(-20.5874324030418,5.03238820704158,
7.19945335934839));
#129127=CARTESIAN_POINT('Ctrl Pts',(-20.580723591589,5.04200983657999,7.34241033440097));
#129128=CARTESIAN_POINT('Ctrl Pts',(-20.5740068318481,5.05164286537795,
7.48553667823434));
#129129=CARTESIAN_POINT('Ctrl Pts',(-20.5672900721073,5.06731422089046,
7.62816930839523));
#129130=CARTESIAN_POINT('Ctrl Pts',(-20.5605733123664,5.088940140337,7.76977743611652));
#129131=CARTESIAN_POINT('Ctrl Pts',(-20.5538521696223,5.11058017171842,
7.91147796983615));
#129132=CARTESIAN_POINT('Ctrl Pts',(-20.5471310268781,5.1381824435197,8.05215230563782));
#129133=CARTESIAN_POINT('Ctrl Pts',(-20.540409884134,5.17161234851655,8.19128125783457));
#129134=CARTESIAN_POINT('Ctrl Pts',(-20.5336788198585,5.20509160164702,
8.33061558764527));
#129135=CARTESIAN_POINT('Ctrl Pts',(-20.526947755583,5.24441557450116,8.46839962056655));
#129136=CARTESIAN_POINT('Ctrl Pts',(-20.5202166913075,5.28939995726619,
8.60412985020796));
#129137=CARTESIAN_POINT('Ctrl Pts',(-20.5164822050006,5.31435790664587,
8.67943483368136));
#129138=CARTESIAN_POINT('Ctrl Pts',(-20.5127477186938,5.34105737182238,
8.7541079689008));
#129139=CARTESIAN_POINT('Ctrl Pts',(-20.5090132323869,5.36946062600318,
8.82806623457683));
#129140=CARTESIAN_POINT('Ctrl Pts',(-20.502520363616,5.41884321490794,8.95665187503696));
#129141=CARTESIAN_POINT('Ctrl Pts',(-20.4960274948451,5.47353574030531,
9.08348391875456));
#129142=CARTESIAN_POINT('Ctrl Pts',(-20.4895346260742,5.53339495200478,
9.20808047584159));
#129143=CARTESIAN_POINT('Ctrl Pts',(-20.4855564273429,5.57007085728481,
9.28442113246241));
#129144=CARTESIAN_POINT('Ctrl Pts',(-20.4815782286116,5.60868536043436,
9.35992276697046));
#129145=CARTESIAN_POINT('Ctrl Pts',(-20.4776000298804,5.6491961756188,9.4344770775744));
#129146=CARTESIAN_POINT('Origin',(-26.8463464956315,10.1295,7.));
#129147=CARTESIAN_POINT('',(-18.8525174996886,5.6491961756188,9.4344770775744));
#129148=CARTESIAN_POINT('',(-18.977821433234,5.64904402747702,9.43455986027809));
#129149=CARTESIAN_POINT('',(-26.8463464956315,5.6491961756188,9.4344770775744));
#129150=CARTESIAN_POINT('',(-20.0963464956032,10.1297172757599,12.0989999953708));
#129151=CARTESIAN_POINT('Ctrl Pts',(-20.0963464956032,10.1297172757598,
12.0989999953708));
#129152=CARTESIAN_POINT('Ctrl Pts',(-20.089015871315,10.2862367018524,12.0989933258518));
#129153=CARTESIAN_POINT('Ctrl Pts',(-20.0816852470269,10.4427270477282,
12.0917755131971));
#129154=CARTESIAN_POINT('Ctrl Pts',(-20.0743546227387,10.5985501666255,
12.0773805196369));
#129155=CARTESIAN_POINT('Ctrl Pts',(-20.0698740478804,10.6937913250079,
12.06858210852));
#129156=CARTESIAN_POINT('Ctrl Pts',(-20.0653934730221,10.7887832630484,
12.0571034512937));
#129157=CARTESIAN_POINT('Ctrl Pts',(-20.0609128981638,10.883381113265,12.0429618546111));
#129158=CARTESIAN_POINT('Ctrl Pts',(-20.0540299000486,11.0287010432615,
12.0212377262588));
#129159=CARTESIAN_POINT('Ctrl Pts',(-20.0471469019333,11.1731216585732,
11.9932218786075));
#129160=CARTESIAN_POINT('Ctrl Pts',(-20.040263903818,11.3160889030018,11.959012782326));
#129161=CARTESIAN_POINT('Ctrl Pts',(-20.0333828335523,11.4590161039285,
11.924813267624));
#129162=CARTESIAN_POINT('Ctrl Pts',(-20.0265017632867,11.6004904149984,
11.8844240428383));
#129163=CARTESIAN_POINT('Ctrl Pts',(-20.019620693021,11.7399691658932,11.837994425969));
#129164=CARTESIAN_POINT('Ctrl Pts',(-20.0127398324751,11.8794436657853,
11.7915662241714));
#129165=CARTESIAN_POINT('Ctrl Pts',(-20.0058589719292,12.0169224023365,
11.7390981002918));
#129166=CARTESIAN_POINT('Ctrl Pts',(-19.9989781113832,12.1518786132926,
11.6807890087566));
#129167=CARTESIAN_POINT('Ctrl Pts',(-19.9920977747547,12.2868245485124,
11.6224843569492));
#129168=CARTESIAN_POINT('Ctrl Pts',(-19.9852174381262,12.419248029891,11.5583397622004));
#129169=CARTESIAN_POINT('Ctrl Pts',(-19.9783371014977,12.5486430535138,
11.4886019969068));
#129170=CARTESIAN_POINT('Ctrl Pts',(-19.9714550222469,12.6780708497566,
11.4188465687294));
#129171=CARTESIAN_POINT('Ctrl Pts',(-19.964572942996,12.8044683557619,11.3434953008952));
#129172=CARTESIAN_POINT('Ctrl Pts',(-19.9576908637452,12.9273544175526,
11.2628407967201));
#129173=CARTESIAN_POINT('Ctrl Pts',(-19.9533163269153,13.0054659276911,
11.2115734273474));
#129174=CARTESIAN_POINT('Ctrl Pts',(-19.9489417900855,13.0821591944104,
11.1581642466885));
#129175=CARTESIAN_POINT('Ctrl Pts',(-19.9445672532557,13.1573167585015,
11.1026974878654));
#129176=CARTESIAN_POINT('Ctrl Pts',(-19.9376178346047,13.2767125706703,
11.014582621476));
#129177=CARTESIAN_POINT('Ctrl Pts',(-19.9306684159537,13.392276360347,10.9212397631479));
#129178=CARTESIAN_POINT('Ctrl Pts',(-19.9237189973027,13.5035591632226,
10.8230257340323));
#129179=CARTESIAN_POINT('Ctrl Pts',(-19.9167707096019,13.6148238559054,
10.724827688294));
#129180=CARTESIAN_POINT('Ctrl Pts',(-19.9098224219011,13.7218087066573,
10.6217602701984));
#129181=CARTESIAN_POINT('Ctrl Pts',(-19.9028741342004,13.8240989854157,
10.5142195914549));
#129182=CARTESIAN_POINT('Ctrl Pts',(-19.8959254836163,13.9263946064161,
10.4066732962605));
#129183=CARTESIAN_POINT('Ctrl Pts',(-19.8889768330322,14.0239949372702,
10.2946535083665));
#129184=CARTESIAN_POINT('Ctrl Pts',(-19.8820281824482,14.116522779692,10.1785925115084));
#129185=CARTESIAN_POINT('Ctrl Pts',(-19.8750798802786,14.209045982645,10.0625373341027));
#129186=CARTESIAN_POINT('Ctrl Pts',(-19.8681315781091,14.2964970028861,
9.9424416099158));
#129187=CARTESIAN_POINT('Ctrl Pts',(-19.8611832759396,14.3785395224088,
9.81876996879985));
#129188=CARTESIAN_POINT('Ctrl Pts',(-19.8542335347365,14.4605990334123,
9.69507271457101));
#129189=CARTESIAN_POINT('Ctrl Pts',(-19.8472837935334,14.5372476244609,
9.56779833651679));
#129190=CARTESIAN_POINT('Ctrl Pts',(-19.8403340523302,14.6081924776181,
9.43744019227688));
#129191=CARTESIAN_POINT('Ctrl Pts',(-19.8362965710027,14.6494081878925,
9.36170808112577));
#129192=CARTESIAN_POINT('Ctrl Pts',(-19.8322590896751,14.6886996717564,
9.28493568412992));
#129193=CARTESIAN_POINT('Ctrl Pts',(-19.8282216083475,14.7260166271649,
9.20722357186493));
#129194=CARTESIAN_POINT('Ctrl Pts',(-19.8212896270348,14.7900863816857,
9.07379907617413));
#129195=CARTESIAN_POINT('Ctrl Pts',(-19.8143576457221,14.8483539160099,
8.93755987242083));
#129196=CARTESIAN_POINT('Ctrl Pts',(-19.8074256644093,14.9005897744139,
8.79902845015939));
#129197=CARTESIAN_POINT('Ctrl Pts',(-19.800494999141,14.9528157157817,8.66052332824371));
#129198=CARTESIAN_POINT('Ctrl Pts',(-19.7935643338727,14.9990121492195,
8.51972716550497));
#129199=CARTESIAN_POINT('Ctrl Pts',(-19.7866336686044,15.0389982277045,
8.37718123432116));
#129200=CARTESIAN_POINT('Ctrl Pts',(-19.7797027424108,15.0789858115835,
8.23462993657493));
#129201=CARTESIAN_POINT('Ctrl Pts',(-19.7727718162171,15.1127624801018,
8.09032905625727));
#129202=CARTESIAN_POINT('Ctrl Pts',(-19.7658408900234,15.1401974670158,
7.94483432094795));
#129203=CARTESIAN_POINT('Ctrl Pts',(-19.7589103257021,15.1676310215149,
7.79934718210023));
#129204=CARTESIAN_POINT('Ctrl Pts',(-19.7519797613807,15.1887234966507,
7.65266663834769));
#129205=CARTESIAN_POINT('Ctrl Pts',(-19.7450491970594,15.2033953868547,
7.50535789620315));
#129206=CARTESIAN_POINT('Ctrl Pts',(-19.7381170569175,15.2180706130446,
7.35801566008556));
#129207=CARTESIAN_POINT('Ctrl Pts',(-19.7311849167757,15.2263223045308,
7.21004526955849));
#129208=CARTESIAN_POINT('Ctrl Pts',(-19.7242527766338,15.228122843019,7.06201697061806));
#129209=CARTESIAN_POINT('Ctrl Pts',(-19.7201271722356,15.2291944182259,
6.97391918426839));
#129210=CARTESIAN_POINT('Ctrl Pts',(-19.7160015678375,15.2279820313568,
6.88580095229293));
#129211=CARTESIAN_POINT('Ctrl Pts',(-19.7118759634393,15.2244886255794,
6.79778252989406));
#129212=CARTESIAN_POINT('Ctrl Pts',(-19.7049446779354,15.2186194751504,
6.64990581745022));
#129213=CARTESIAN_POINT('Ctrl Pts',(-19.6980133924316,15.2063069875029,
6.50225841772228));
#129214=CARTESIAN_POINT('Ctrl Pts',(-19.6910821069277,15.1875929083198,
6.35540933081153));
#129215=CARTESIAN_POINT('Ctrl Pts',(-19.6841521797915,15.1688824966527,
6.20858902284121));
#129216=CARTESIAN_POINT('Ctrl Pts',(-19.6772222526554,15.1437730382402,
6.06256704375078));
#129217=CARTESIAN_POINT('Ctrl Pts',(-19.6702923255192,15.1123580259662,
5.91790624571419));
#129218=CARTESIAN_POINT('Ctrl Pts',(-19.6633621941248,15.0809420877409,
5.77324118382936));
#129219=CARTESIAN_POINT('Ctrl Pts',(-19.6564320627304,15.0432202905388,
5.62993770751524));
#129220=CARTESIAN_POINT('Ctrl Pts',(-19.649501931336,14.9993371489926,5.4885480019888));
#129221=CARTESIAN_POINT('Ctrl Pts',(-19.6425721921158,14.9554564907814,
5.34716629766733));
#129222=CARTESIAN_POINT('Ctrl Pts',(-19.6356424528956,14.9054152848104,
5.20769846335047));
#129223=CARTESIAN_POINT('Ctrl Pts',(-19.6287127136755,14.8494077822416,
5.07068107169002));
#129224=CARTESIAN_POINT('Ctrl Pts',(-19.6217814385137,14.7933878658937,
4.93363331081897));
#129225=CARTESIAN_POINT('Ctrl Pts',(-19.614850163352,14.7313991358923,4.7990373843918));
#129226=CARTESIAN_POINT('Ctrl Pts',(-19.6079188881903,14.6636840544642,
4.66741003169391));
#129227=CARTESIAN_POINT('Ctrl Pts',(-19.6037893649705,14.6233406840804,
4.58898893360848));
#129228=CARTESIAN_POINT('Ctrl Pts',(-19.5996598417508,14.5809656252747,
4.51162113845325));
#129229=CARTESIAN_POINT('Ctrl Pts',(-19.5955303185311,14.5366179506424,
4.43541185194857));
#129230=CARTESIAN_POINT('Ctrl Pts',(-19.5885944784662,14.4621327468707,
4.30741271148285));
#129231=CARTESIAN_POINT('Ctrl Pts',(-19.5816586384013,14.3820549717155,
4.1826393380251));
#129232=CARTESIAN_POINT('Ctrl Pts',(-19.5747227983364,14.2966886979184,
4.06157536153454));
#129233=CARTESIAN_POINT('Ctrl Pts',(-19.5677882396657,14.2113381955128,
3.94053375157444));
#129234=CARTESIAN_POINT('Ctrl Pts',(-19.560853680995,14.1207013340158,3.82320044090237));
#129235=CARTESIAN_POINT('Ctrl Pts',(-19.5539191223243,14.0251250075616,
3.71002936176316));
#129236=CARTESIAN_POINT('Ctrl Pts',(-19.5469842888657,13.9295448938135,
3.59685379812276));
#129237=CARTESIAN_POINT('Ctrl Pts',(-19.5400494554072,13.829025134011,3.48784105031471));
#129238=CARTESIAN_POINT('Ctrl Pts',(-19.5331146219486,13.7239526913764,
3.38341171136981));
#129239=CARTESIAN_POINT('Ctrl Pts',(-19.5261801519479,13.6188857556362,
3.27898784561402));
#129240=CARTESIAN_POINT('Ctrl Pts',(-19.5192456819471,13.5092668493917,
3.17914714004377));
#129241=CARTESIAN_POINT('Ctrl Pts',(-19.5123112119463,13.3955195536049,
3.08427308466612));
#129242=CARTESIAN_POINT('Ctrl Pts',(-19.5053752028742,13.2817470121674,
2.98937797246017));
#129243=CARTESIAN_POINT('Ctrl Pts',(-19.498439193802,13.1638445039637,2.89945192455088));
#129244=CARTESIAN_POINT('Ctrl Pts',(-19.4915031847299,13.0422689075063,
2.81483831955505));
#129245=CARTESIAN_POINT('Ctrl Pts',(-19.4873970143609,12.9702952254405,
2.76474641886229));
#129246=CARTESIAN_POINT('Ctrl Pts',(-19.4832908439919,12.8970348335195,
2.7165156038769));
#129247=CARTESIAN_POINT('Ctrl Pts',(-19.4791846736229,12.8225874034969,
2.67021002390112));
#129248=CARTESIAN_POINT('Ctrl Pts',(-19.4722525221646,12.6969031736126,
2.59203565096661));
#129249=CARTESIAN_POINT('Ctrl Pts',(-19.4653203707063,12.5677907388499,
2.51932374374962));
#129250=CARTESIAN_POINT('Ctrl Pts',(-19.4583882192479,12.4357445771247,
2.45235918849313));
#129251=CARTESIAN_POINT('Ctrl Pts',(-19.4514574046156,12.3037238797516,
2.38540754697065));
#129252=CARTESIAN_POINT('Ctrl Pts',(-19.4445265899833,12.1687708790819,
2.32420119569282));
#129253=CARTESIAN_POINT('Ctrl Pts',(-19.437595775351,12.0314040081221,2.2689787419745));
#129254=CARTESIAN_POINT('Ctrl Pts',(-19.4306647326403,11.8940326167084,
2.21375447100176));
#129255=CARTESIAN_POINT('Ctrl Pts',(-19.4237336899295,11.7542475017451,
2.16451461821821));
#129256=CARTESIAN_POINT('Ctrl Pts',(-19.4168026472187,11.6125869069858,
2.12144957735116));
#129257=CARTESIAN_POINT('Ctrl Pts',(-19.4098719853274,11.4709340956326,
2.07838690265164));
#129258=CARTESIAN_POINT('Ctrl Pts',(-19.4029413234362,11.3274063275018,
2.04149845637549));
#129259=CARTESIAN_POINT('Ctrl Pts',(-19.3960106615449,11.1825568421866,
2.01092470620818));
#129260=CARTESIAN_POINT('Ctrl Pts',(-19.3890784541281,11.0376750556869,
1.98034413814747));
#129261=CARTESIAN_POINT('Ctrl Pts',(-19.3821462467112,10.8914712869162,
1.95608114825949));
#129262=CARTESIAN_POINT('Ctrl Pts',(-19.3752140392943,10.7445094240285,
1.93822517210058));
#129263=CARTESIAN_POINT('Ctrl Pts',(-19.3710890357678,10.6570599052499,
1.92759999022186));
#129264=CARTESIAN_POINT('Ctrl Pts',(-19.3669640322412,10.5693421308198,
1.91924244470383));
#129265=CARTESIAN_POINT('Ctrl Pts',(-19.3628390287147,10.481475913415,1.91316267643876));
#129266=CARTESIAN_POINT('Ctrl Pts',(-19.3559048049855,10.3337708252122,
1.90294244920731));
#129267=CARTESIAN_POINT('Ctrl Pts',(-19.3489705812563,10.1855950223114,
1.89915811409712));
#129268=CARTESIAN_POINT('Ctrl Pts',(-19.3420363575271,10.0375191660747,
1.90182968838914));
#129269=CARTESIAN_POINT('Ctrl Pts',(-19.3351034415158,9.8894712353064,1.9045007588518));
#129270=CARTESIAN_POINT('Ctrl Pts',(-19.3281705255045,9.74152354381111,
1.9136253036207));
#129271=CARTESIAN_POINT('Ctrl Pts',(-19.3212376094931,9.59424623169765,
1.9291712310986));
#129272=CARTESIAN_POINT('Ctrl Pts',(-19.3143044421616,9.44696358073864,
1.9447177221209));
#129273=CARTESIAN_POINT('Ctrl Pts',(-19.30737127483,9.30035168675085,1.96668603024645));
#129274=CARTESIAN_POINT('Ctrl Pts',(-19.3004381074985,9.15497560566773,
1.99499218733364));
#129275=CARTESIAN_POINT('Ctrl Pts',(-19.2935053129045,9.00960734022225,
2.02329682263908));
#129276=CARTESIAN_POINT('Ctrl Pts',(-19.2865725183105,8.86547507891971,
2.05793856101137));
#129277=CARTESIAN_POINT('Ctrl Pts',(-19.2796397237165,8.72313373977314,
2.09878230007118));
#129278=CARTESIAN_POINT('Ctrl Pts',(-19.2727053897295,8.58076079443217,
2.13963510828241));
#129279=CARTESIAN_POINT('Ctrl Pts',(-19.2657710557426,8.44017988357931,
2.18669257768057));
#129280=CARTESIAN_POINT('Ctrl Pts',(-19.2588367217556,8.30193143109621,
2.23976953016401));
#129281=CARTESIAN_POINT('Ctrl Pts',(-19.2547222757726,8.21990253098119,
2.27126242542232));
#129282=CARTESIAN_POINT('Ctrl Pts',(-19.2506078297895,8.13869448353687,
2.30487357806509));
#129283=CARTESIAN_POINT('Ctrl Pts',(-19.2464933838065,8.05841702068354,
2.34055622495714));
#129284=CARTESIAN_POINT('Ctrl Pts',(-19.2395600669797,7.92314022125396,
2.40068560741598));
#129285=CARTESIAN_POINT('Ctrl Pts',(-19.232626750153,7.79046037418254,2.4667205608979));
#129286=CARTESIAN_POINT('Ctrl Pts',(-19.2256934333262,7.66089097296183,
2.53841166493079));
#129287=CARTESIAN_POINT('Ctrl Pts',(-19.218761436208,7.53134623437504,2.61008912306088));
#129288=CARTESIAN_POINT('Ctrl Pts',(-19.2118294390899,7.40491104954959,
2.68742042376904));
#129289=CARTESIAN_POINT('Ctrl Pts',(-19.2048974419717,7.28207405548853,
2.77011034534907));
#129290=CARTESIAN_POINT('Ctrl Pts',(-19.1979652025665,7.1592327680301,2.8528031571064));
#129291=CARTESIAN_POINT('Ctrl Pts',(-19.1910329631612,7.03999019913484,
2.94085478267516));
#129292=CARTESIAN_POINT('Ctrl Pts',(-19.184100723756,6.92480620440643,3.03392654171861));
#129293=CARTESIAN_POINT('Ctrl Pts',(-19.177168859976,6.8096284509534,3.12699325764406));
#129294=CARTESIAN_POINT('Ctrl Pts',(-19.170236996196,6.69850908820766,3.22507935421226));
#129295=CARTESIAN_POINT('Ctrl Pts',(-19.163305132416,6.5918750714188,3.32780571528673));
#129296=CARTESIAN_POINT('Ctrl Pts',(-19.1563717255625,6.48521731727435,
3.43055494384976));
#129297=CARTESIAN_POINT('Ctrl Pts',(-19.1494383187091,6.38304714234844,
3.53794627142115));
#129298=CARTESIAN_POINT('Ctrl Pts',(-19.1425049118557,6.28575524711227,
3.64956312182307));
#129299=CARTESIAN_POINT('Ctrl Pts',(-19.1383858542032,6.22795524574662,
3.71587341509055));
#129300=CARTESIAN_POINT('Ctrl Pts',(-19.1342667965508,6.17187627667052,
3.7836743770029));
#129301=CARTESIAN_POINT('Ctrl Pts',(-19.1301477388983,6.11759365881622,
3.8528729753044));
#129302=CARTESIAN_POINT('Ctrl Pts',(-19.1232141282746,6.02621971662068,
3.96935499056361));
#129303=CARTESIAN_POINT('Ctrl Pts',(-19.1162805176509,5.93990636053414,
4.08983920703717));
#129304=CARTESIAN_POINT('Ctrl Pts',(-19.1093469070272,5.85899051470744,
4.21386473120448));
#129305=CARTESIAN_POINT('Ctrl Pts',(-19.1024146126326,5.77809002939035,
4.3378667112163));
#129306=CARTESIAN_POINT('Ctrl Pts',(-19.095482318238,5.70258519057678,4.46540838095846));
#129307=CARTESIAN_POINT('Ctrl Pts',(-19.0885500238434,5.63276951068097,
4.5960000194616));
#129308=CARTESIAN_POINT('Ctrl Pts',(-19.0816174848406,5.56295136731649,
4.72659626593262));
#129309=CARTESIAN_POINT('Ctrl Pts',(-19.0746849458378,5.49882294336051,
4.86024240657262));
#129310=CARTESIAN_POINT('Ctrl Pts',(-19.067752406835,5.44063196898206,4.99642380037644));
#129311=CARTESIAN_POINT('Ctrl Pts',(-19.0608202428625,5.38244414256678,
5.13259782716129));
#129312=CARTESIAN_POINT('Ctrl Pts',(-19.0538880788899,5.33019325204807,
5.27130652831807));
#129313=CARTESIAN_POINT('Ctrl Pts',(-19.0469559149174,5.28407902177485,
5.41201494220643));
#129314=CARTESIAN_POINT('Ctrl Pts',(-19.0400222095796,5.2379545380122,5.55275464258111));
#129315=CARTESIAN_POINT('Ctrl Pts',(-19.0330885042419,5.19796954390401,
5.69549462988479));
#129316=CARTESIAN_POINT('Ctrl Pts',(-19.0261547989042,5.1642741877754,5.83968382170268));
#129317=CARTESIAN_POINT('Ctrl Pts',(-19.0220372305995,5.1442642618192,5.92531031103094));
#129318=CARTESIAN_POINT('Ctrl Pts',(-19.0179196622948,5.12647145780716,
6.01144759299916));
#129319=CARTESIAN_POINT('Ctrl Pts',(-19.0138020939901,5.11091873588374,
6.09797832871864));
#129320=CARTESIAN_POINT('Ctrl Pts',(-19.0068685366575,5.08472956762835,
6.24368709970922));
#129321=CARTESIAN_POINT('Ctrl Pts',(-18.9999349793249,5.06488588872228,
6.39056232944993));
#129322=CARTESIAN_POINT('Ctrl Pts',(-18.9930014219922,5.05146956995229,
6.53803901516524));
#129323=CARTESIAN_POINT('Ctrl Pts',(-18.9860691811566,5.03805579858218,
6.68548769900486));
#129324=CARTESIAN_POINT('Ctrl Pts',(-18.9791369403209,5.03106698243318,
6.83353728193027));
#129325=CARTESIAN_POINT('Ctrl Pts',(-18.9722046994853,5.03053313522663,
6.981617618673));
#129326=CARTESIAN_POINT('Ctrl Pts',(-18.9652722139179,5.02999926917346,
7.12970318315559));
#129327=CARTESIAN_POINT('Ctrl Pts',(-18.9583397283506,5.03592083259744,
7.27781917307016));
#129328=CARTESIAN_POINT('Ctrl Pts',(-18.9514072427832,5.04827571738032,
7.425394863293));
#129329=CARTESIAN_POINT('Ctrl Pts',(-18.9444751320469,5.06062993414973,
7.5729625742793));
#129330=CARTESIAN_POINT('Ctrl Pts',(-18.9375430213105,5.07941674773547,
7.71998971467153));
#129331=CARTESIAN_POINT('Ctrl Pts',(-18.9306109105742,5.10456211729908,
7.86591008482244));
#129332=CARTESIAN_POINT('Ctrl Pts',(-18.9236772576965,5.1297130807884,8.01186291692259));
#129333=CARTESIAN_POINT('Ctrl Pts',(-18.9167436048189,5.16122537054665,
8.15670816091301));
#129334=CARTESIAN_POINT('Ctrl Pts',(-18.9098099519412,5.19897359234506,
8.29988858884801));
#129335=CARTESIAN_POINT('Ctrl Pts',(-18.9056921176548,5.22139192287256,
8.38492216144007));
#129336=CARTESIAN_POINT('Ctrl Pts',(-18.9015742833684,5.24600873413893,
8.46936874424738));
#129337=CARTESIAN_POINT('Ctrl Pts',(-18.8974564490819,5.27278935781425,
8.55311388445269));
#129338=CARTESIAN_POINT('Ctrl Pts',(-18.8905229466365,5.31788187655751,
8.69412177695536));
#129339=CARTESIAN_POINT('Ctrl Pts',(-18.883589444191,5.36912726528092,8.83318887245178));
#129340=CARTESIAN_POINT('Ctrl Pts',(-18.8766559417456,5.42633328808934,
8.96977762196028));
#129341=CARTESIAN_POINT('Ctrl Pts',(-18.8697236783249,5.48352908811637,
9.10634196290375));
#129342=CARTESIAN_POINT('Ctrl Pts',(-18.8627914149043,5.54668326980763,
9.24042853657159));
#129343=CARTESIAN_POINT('Ctrl Pts',(-18.8558591514836,5.61555536291239,
9.37151951569199));
#129344=CARTESIAN_POINT('Ctrl Pts',(-18.8547452675519,5.62662180877491,
9.39258336257253));
#129345=CARTESIAN_POINT('Ctrl Pts',(-18.8536313836203,5.63783578315601,
9.41356991427992));
#129346=CARTESIAN_POINT('Ctrl Pts',(-18.8525174996886,5.6491961756188,9.4344770775744));
#129347=CARTESIAN_POINT('Ctrl Pts',(-20.35256332674,5.6491961756188,9.4344770775744));
#129348=CARTESIAN_POINT('Ctrl Pts',(-20.3452864953739,5.72333205001175,
9.57091345835869));
#129349=CARTESIAN_POINT('Ctrl Pts',(-20.3380096640078,5.80368599783711,
9.70392825010587));
#129350=CARTESIAN_POINT('Ctrl Pts',(-20.3307328326417,5.88992663933501,
9.83298759607941));
#129351=CARTESIAN_POINT('Ctrl Pts',(-20.3234537917686,5.97619346658475,
9.96208612909918));
#129352=CARTESIAN_POINT('Ctrl Pts',(-20.3161747508955,6.06835041676543,
10.0872266066909));
#129353=CARTESIAN_POINT('Ctrl Pts',(-20.3088957100224,6.16602295733249,
10.20790441445));
#129354=CARTESIAN_POINT('Ctrl Pts',(-20.3037985360084,6.23441849794657,
10.2924094744585));
#129355=CARTESIAN_POINT('Ctrl Pts',(-20.2987013619943,6.30551773923257,
10.3747268589894));
#129356=CARTESIAN_POINT('Ctrl Pts',(-20.2936041879802,6.3791801760683,10.4546927820321));
#129357=CARTESIAN_POINT('Ctrl Pts',(-20.2868779809018,6.47638478448219,
10.5602154414733));
#129358=CARTESIAN_POINT('Ctrl Pts',(-20.2801517738235,6.57810999823997,
10.6617018342539));
#129359=CARTESIAN_POINT('Ctrl Pts',(-20.2734255667451,6.68398946099055,
10.7587575241793));
#129360=CARTESIAN_POINT('Ctrl Pts',(-20.2667029434128,6.7898125108012,10.8557615025012));
#129361=CARTESIAN_POINT('Ctrl Pts',(-20.2599803200806,6.89978512979311,
10.9483392324725));
#129362=CARTESIAN_POINT('Ctrl Pts',(-20.2532576967484,7.01350428426586,
11.0361332608731));
#129363=CARTESIAN_POINT('Ctrl Pts',(-20.2465367266287,7.12719547317678,
11.1239056991614));
#129364=CARTESIAN_POINT('Ctrl Pts',(-20.2398157565091,7.24463107375143,
11.2068965514905));
#129365=CARTESIAN_POINT('Ctrl Pts',(-20.2330947863894,7.36537511122738,
11.2847887461656));
#129366=CARTESIAN_POINT('Ctrl Pts',(-20.2263749847876,7.48609815596555,
11.3626673983881));
#129367=CARTESIAN_POINT('Ctrl Pts',(-20.2196551831858,7.61012818104768,
11.435448961937));
#129368=CARTESIAN_POINT('Ctrl Pts',(-20.212935381584,7.73700061751279,11.5028599472778));
#129369=CARTESIAN_POINT('Ctrl Pts',(-20.2062137509067,7.86390758762793,
11.570289281343));
#129370=CARTESIAN_POINT('Ctrl Pts',(-20.1994921202293,7.99365819072875,
11.6323449420533));
#129371=CARTESIAN_POINT('Ctrl Pts',(-20.1927704895519,8.12576338186563,
11.6887994801599));
#129372=CARTESIAN_POINT('Ctrl Pts',(-20.1875998407253,8.2273859767871,11.732227422757));
#129373=CARTESIAN_POINT('Ctrl Pts',(-20.1824291918987,8.33040137579851,
11.7723418012303));
#129374=CARTESIAN_POINT('Ctrl Pts',(-20.1772585430721,8.43457914043762,
11.809058564815));
#129375=CARTESIAN_POINT('Ctrl Pts',(-20.1702026804407,8.57674002221321,
11.8591622266207));
#129376=CARTESIAN_POINT('Ctrl Pts',(-20.1631468178092,8.72111220267323,
11.9029539856882));
#129377=CARTESIAN_POINT('Ctrl Pts',(-20.1560909551778,8.86712880719496,
11.9402651721923));
#129378=CARTESIAN_POINT('Ctrl Pts',(-20.1490348696706,9.01315002398955,
11.9775775372567));
#129379=CARTESIAN_POINT('Ctrl Pts',(-20.1419787841634,9.16081547203784,
12.0084088496475));
#129380=CARTESIAN_POINT('Ctrl Pts',(-20.1349226986562,9.30954582988,12.0326410719326));
#129381=CARTESIAN_POINT('Ctrl Pts',(-20.1278650246748,9.45830967007435,
12.0568787494039));
#129382=CARTESIAN_POINT('Ctrl Pts',(-20.1208073506934,9.60813859809027,
12.0745143189556));
#129383=CARTESIAN_POINT('Ctrl Pts',(-20.1137496767119,9.75844499148024,
12.085481214266));
#129384=CARTESIAN_POINT('Ctrl Pts',(-20.1079486163518,9.8819894429335,12.094495461995));
#129385=CARTESIAN_POINT('Ctrl Pts',(-20.1021475559916,10.0058562501456,
12.0990052732534));
#129386=CARTESIAN_POINT('Ctrl Pts',(-20.0963464956315,10.1297172751558,
12.0989999953708));
#129387=CARTESIAN_POINT('',(-20.2216535043684,10.1252586289357,12.098998236004));
#129388=CARTESIAN_POINT('Ctrl Pts',(-20.4776000298804,5.6491961756188,9.4344770775744));
#129389=CARTESIAN_POINT('Ctrl Pts',(-20.4711196343864,5.71518737462922,
9.55592435839926));
#129390=CARTESIAN_POINT('Ctrl Pts',(-20.4646392388925,5.78621302249013,
9.67485669317108));
#129391=CARTESIAN_POINT('Ctrl Pts',(-20.4581588433985,5.86205110746356,
9.7908208379596));
#129392=CARTESIAN_POINT('Ctrl Pts',(-20.4516842460785,5.93782133818231,
9.90668122669182));
#129393=CARTESIAN_POINT('Ctrl Pts',(-20.4452096487584,6.01839522353272,
10.0195783739772));
#129394=CARTESIAN_POINT('Ctrl Pts',(-20.4387350514384,6.10350485213512,
10.1290835829949));
#129395=CARTESIAN_POINT('Ctrl Pts',(-20.4319678385689,6.1924609594459,10.243537814372));
#129396=CARTESIAN_POINT('Ctrl Pts',(-20.4252006256994,6.28637217257196,
10.3542859469112));
#129397=CARTESIAN_POINT('Ctrl Pts',(-20.4184334128299,6.38488171041246,
10.4608719804822));
#129398=CARTESIAN_POINT('Ctrl Pts',(-20.4119646414821,6.47904686941601,
10.562757452882));
#129399=CARTESIAN_POINT('Ctrl Pts',(-20.4054958701343,6.5774131285831,10.6608397694563));
#129400=CARTESIAN_POINT('Ctrl Pts',(-20.3990270987865,6.67962808601849,
10.7547549556691));
#129401=CARTESIAN_POINT('Ctrl Pts',(-20.392558785631,6.7818358034224,10.8486634897351));
#129402=CARTESIAN_POINT('Ctrl Pts',(-20.3860904724756,6.88789138192054,
10.9384052085303));
#129403=CARTESIAN_POINT('Ctrl Pts',(-20.3796221593201,6.99740680186872,
11.0236542095737));
#129404=CARTESIAN_POINT('Ctrl Pts',(-20.3731528261516,7.10693949172239,
11.1089166538581));
#129405=CARTESIAN_POINT('Ctrl Pts',(-20.366683492983,7.21993279133841,11.189684725096));
#129406=CARTESIAN_POINT('Ctrl Pts',(-20.3602141598145,7.33596740778494,
11.2656742323145));
#129407=CARTESIAN_POINT('Ctrl Pts',(-20.3537423276633,7.45204684623852,
11.3416930928617));
#129408=CARTESIAN_POINT('Ctrl Pts',(-20.3472704955121,7.57116960235738,
11.4129294991824));
#129409=CARTESIAN_POINT('Ctrl Pts',(-20.3407986633609,7.69288983290592,
11.4791441027962));
#129410=CARTESIAN_POINT('Ctrl Pts',(-20.3343191314151,7.81475487882639,
11.5454374845424));
#129411=CARTESIAN_POINT('Ctrl Pts',(-20.3278395994692,7.9392232143583,11.60669694793));
#129412=CARTESIAN_POINT('Ctrl Pts',(-20.3213600675234,8.06582667605563,
11.6627302529784));
#129413=CARTESIAN_POINT('Ctrl Pts',(-20.3148760101054,8.19251856087417,
11.7188026931316));
#129414=CARTESIAN_POINT('Ctrl Pts',(-20.3083919526874,8.321348168011,11.7696415644407));
#129415=CARTESIAN_POINT('Ctrl Pts',(-20.3019078952694,8.45183129723872,
11.8151042277167));
#129416=CARTESIAN_POINT('Ctrl Pts',(-20.2954140890341,8.58251060859469,
11.860635244366));
#129417=CARTESIAN_POINT('Ctrl Pts',(-20.2889202827989,8.71484802107036,
11.9007738090514));
#129418=CARTESIAN_POINT('Ctrl Pts',(-20.2824264765636,8.84834794582099,
11.9354280882283));
#129419=CARTESIAN_POINT('Ctrl Pts',(-20.2803916318992,8.8901803627013,11.946287062538));
#129420=CARTESIAN_POINT('Ctrl Pts',(-20.2783567872349,8.93212688187923,
11.956607921674));
#129421=CARTESIAN_POINT('Ctrl Pts',(-20.2763219425705,8.97417216558045,
11.9663888888221));
#129422=CARTESIAN_POINT('Ctrl Pts',(-20.2664274954747,9.17861766576668,
12.0139489132734));
#129423=CARTESIAN_POINT('Ctrl Pts',(-20.2565330483789,9.38595698020578,
12.0488706803317));
#129424=CARTESIAN_POINT('Ctrl Pts',(-20.2466386012831,9.59491891455191,
12.0708997291488));
#129425=CARTESIAN_POINT('Ctrl Pts',(-20.2383102356448,9.77080659951878,
12.0894420460094));
#129426=CARTESIAN_POINT('Ctrl Pts',(-20.2299818700066,9.94784426009558,
12.0988506618854));
#129427=CARTESIAN_POINT('Ctrl Pts',(-20.2216535043684,10.1252586289357,
12.098998236004));
#129428=CARTESIAN_POINT('Ctrl Pts',(-20.2216531624029,10.1252652855325,
12.0997546424994));
#129429=CARTESIAN_POINT('Ctrl Pts',(-20.1623123258533,11.389567257658,12.087821313962));
#129430=CARTESIAN_POINT('Ctrl Pts',(-20.0641896076676,13.4904584433699,
11.2892797426427));
#129431=CARTESIAN_POINT('Ctrl Pts',(-19.9272850078459,15.1309521650029,
8.75245213992368));
#129432=CARTESIAN_POINT('Ctrl Pts',(-19.8109393629377,15.377488382025,6.21192549167328));
#129433=CARTESIAN_POINT('Ctrl Pts',(-19.6945937180295,14.3935630371621,
3.84345496751412));
#129434=CARTESIAN_POINT('Ctrl Pts',(-19.5782480731213,12.4208416194932,
2.21543165074234));
#129435=CARTESIAN_POINT('Ctrl Pts',(-19.4619024282132,9.91265035575874,
1.69885130841003));
#129436=CARTESIAN_POINT('Ctrl Pts',(-19.3455567833049,7.45588094355372,
2.41786028132917));
#129437=CARTESIAN_POINT('Ctrl Pts',(-19.2292111383967,5.62120273326431,
4.20319480177778));
#129438=CARTESIAN_POINT('Ctrl Pts',(-19.1128654934885,4.83646615949574,
6.64003369704514));
#129439=CARTESIAN_POINT('Ctrl Pts',(-19.029068925101,5.15885344613513,8.45540706951305));
#129440=CARTESIAN_POINT('Ctrl Pts',(-18.9840542383494,5.58538293497073,
9.31766121934795));
#129441=CARTESIAN_POINT('Ctrl Pts',(-18.977821433234,5.64904402747702,9.43455986027809));
#129442=CARTESIAN_POINT('Origin',(26.8463464956315,10.1295,7.));
#129443=CARTESIAN_POINT('',(23.3525227608221,14.6098038194187,9.43447708670711));
#129444=CARTESIAN_POINT('',(23.4778327564121,14.6092485246327,9.4341754467045));
#129445=CARTESIAN_POINT('',(26.8463464956315,14.6098038194187,9.43447708670711));
#129446=CARTESIAN_POINT('',(23.5339999999999,15.0538811994916,5.6770219948566));
#129447=CARTESIAN_POINT('Ctrl Pts',(23.5339999999999,15.0538811994916,5.6770219948566));
#129448=CARTESIAN_POINT('Ctrl Pts',(23.5270930717027,15.0921506970965,5.8194685009863));
#129449=CARTESIAN_POINT('Ctrl Pts',(23.5201861434054,15.1242415793792,5.96360031998381));
#129450=CARTESIAN_POINT('Ctrl Pts',(23.5132792151082,15.1500258622284,6.10886529262073));
#129451=CARTESIAN_POINT('Ctrl Pts',(23.5063724323829,15.1758096016423,6.25412720362094));
#129452=CARTESIAN_POINT('Ctrl Pts',(23.4994656496576,15.1952869431655,6.40052189108961));
#129453=CARTESIAN_POINT('Ctrl Pts',(23.4925588669324,15.2083811232991,6.54748753012045));
#129454=CARTESIAN_POINT('Ctrl Pts',(23.4856526906085,15.2214741537902,6.69444026586755));
#129455=CARTESIAN_POINT('Ctrl Pts',(23.4787465142847,15.2281851137662,6.84196351862882));
#129456=CARTESIAN_POINT('Ctrl Pts',(23.4718403379609,15.2284891702847,6.98949089349636));
#129457=CARTESIAN_POINT('Ctrl Pts',(23.4649324938645,15.2287933002297,7.13705389474971));
#129458=CARTESIAN_POINT('Ctrl Pts',(23.4580246497681,15.2226874332482,7.28462068429066));
#129459=CARTESIAN_POINT('Ctrl Pts',(23.4511168056718,15.2101988752891,7.43162476601365));
#129460=CARTESIAN_POINT('Ctrl Pts',(23.4457234039484,15.2004482484538,7.54640038292906));
#129461=CARTESIAN_POINT('Ctrl Pts',(23.4403300022249,15.186807817628,7.66083293227476));
#129462=CARTESIAN_POINT('Ctrl Pts',(23.4349366005015,15.1693125726679,7.77465491180164));
#129463=CARTESIAN_POINT('Ctrl Pts',(23.428002553564,15.1468197460705,7.92099056210697));
#129464=CARTESIAN_POINT('Ctrl Pts',(23.4210685066266,15.1179452650816,8.06637109676426));
#129465=CARTESIAN_POINT('Ctrl Pts',(23.4141344596891,15.0827949924592,8.21023539763084));
#129466=CARTESIAN_POINT('Ctrl Pts',(23.4072019007547,15.0476522628654,8.35406882611838));
#129467=CARTESIAN_POINT('Ctrl Pts',(23.4002693418204,15.0062365079439,8.49638634919968));
#129468=CARTESIAN_POINT('Ctrl Pts',(23.393336782886,14.9587043104703,8.63663885073485));
#129469=CARTESIAN_POINT('Ctrl Pts',(23.3864039341192,14.9111701257981,8.77689721586582));
#129470=CARTESIAN_POINT('Ctrl Pts',(23.3794710853524,14.8575190898333,8.91509007250136));
#129471=CARTESIAN_POINT('Ctrl Pts',(23.3725382365856,14.7979572868406,9.05068465663168));
#129472=CARTESIAN_POINT('Ctrl Pts',(23.3658664113311,14.7406380008189,9.18117407032051));
#129473=CARTESIAN_POINT('Ctrl Pts',(23.3591945860766,14.6778450416099,9.30925703459592));
#129474=CARTESIAN_POINT('Ctrl Pts',(23.3525227608221,14.6098038194187,9.43447708670711));
#129475=CARTESIAN_POINT('',(23.534,15.0539061944433,8.32288496556904));
#129476=CARTESIAN_POINT('Origin',(23.534,10.1295,7.));
#129477=CARTESIAN_POINT('Ctrl Pts',(23.534,15.0539061944433,8.32288496556903));
#129478=CARTESIAN_POINT('Ctrl Pts',(23.5152775854706,14.950159911235,8.70907790976189));
#129479=CARTESIAN_POINT('Ctrl Pts',(23.4965551709413,14.8001544393626,9.08275274683618));
#129480=CARTESIAN_POINT('Ctrl Pts',(23.4778327564119,14.6092485246315,9.43417544670676));
#129481=CARTESIAN_POINT('Origin',(26.8463464956315,10.1295,7.));
#129482=CARTESIAN_POINT('',(21.8525208814298,14.6095924811794,9.43436249769606));
#129483=CARTESIAN_POINT('',(21.9778242972865,14.6098038194187,9.43447708670711));
#129484=CARTESIAN_POINT('',(26.8463464956315,14.6098038194187,9.43447708670711));
#129485=CARTESIAN_POINT('',(23.0963464956316,10.1294332246189,12.0990156955494));
#129486=CARTESIAN_POINT('Ctrl Pts',(23.0963464956316,10.1294332206623,12.0993178216526));
#129487=CARTESIAN_POINT('Ctrl Pts',(23.0928642190134,10.0550711278111,12.0993673700521));
#129488=CARTESIAN_POINT('Ctrl Pts',(23.0506000607591,9.15256913101046,12.0800148503643));
#129489=CARTESIAN_POINT('Ctrl Pts',(22.9695540208687,7.44243506000627,11.5744658280441));
#129490=CARTESIAN_POINT('Ctrl Pts',(22.8532083759605,5.61311993670382,9.783588785421));
#129491=CARTESIAN_POINT('Ctrl Pts',(22.7368627310523,4.83541687908909,7.34457045164505));
#129492=CARTESIAN_POINT('Ctrl Pts',(22.6205170861442,5.29040469497751,4.82532063665908));
#129493=CARTESIAN_POINT('Ctrl Pts',(22.504171441236,6.87215451106252,2.81243229447991));
#129494=CARTESIAN_POINT('Ctrl Pts',(22.3878257963277,9.21233876997001,1.77459149097018));
#129495=CARTESIAN_POINT('Ctrl Pts',(22.2714801514196,11.7661169025298,1.95345839105347));
#129496=CARTESIAN_POINT('Ctrl Pts',(22.1551345065114,13.9387381504676,3.30737374765752));
#129497=CARTESIAN_POINT('Ctrl Pts',(22.0387888616032,15.2245708351663,5.52111016209781));
#129498=CARTESIAN_POINT('Ctrl Pts',(21.9379176532427,15.310510332437,7.7389324002892));
#129499=CARTESIAN_POINT('Ctrl Pts',(21.8758283265182,14.8470613098453,8.99675594530229));
#129500=CARTESIAN_POINT('Ctrl Pts',(21.8525208814298,14.6095924811794,9.43436249769606));
#129501=CARTESIAN_POINT('Ctrl Pts',(23.3525227608221,14.6098038194187,9.43447708670711));
#129502=CARTESIAN_POINT('Ctrl Pts',(23.3455889836027,14.5390911345967,9.56461358033825));
#129503=CARTESIAN_POINT('Ctrl Pts',(23.3386552063833,14.4627098494206,9.69165750992628));
#129504=CARTESIAN_POINT('Ctrl Pts',(23.3317214291639,14.3809576871128,9.8151214067407));
#129505=CARTESIAN_POINT('Ctrl Pts',(23.3273446046404,14.3293530771693,9.89305581308964));
#129506=CARTESIAN_POINT('Ctrl Pts',(23.3229677801168,14.2756093228907,9.9695642618301));
#129507=CARTESIAN_POINT('Ctrl Pts',(23.3185909555933,14.2198101839654,10.0445301113552));
#129508=CARTESIAN_POINT('Ctrl Pts',(23.3116576153536,14.1314186084821,10.1632837278912));
#129509=CARTESIAN_POINT('Ctrl Pts',(23.304724275114,14.0378366099381,10.2782059009288));
#129510=CARTESIAN_POINT('Ctrl Pts',(23.2977909348743,13.9394203703912,10.3888505088419));
#129511=CARTESIAN_POINT('Ctrl Pts',(23.2908589149614,13.8410228724023,10.4994740465299));
#129512=CARTESIAN_POINT('Ctrl Pts',(23.2839268950485,13.7377931897414,10.6058213974011));
#129513=CARTESIAN_POINT('Ctrl Pts',(23.2769948751356,13.6301267227303,10.7074807549206));
#129514=CARTESIAN_POINT('Ctrl Pts',(23.2700626140937,13.5224565105608,10.8091436486423));
#129515=CARTESIAN_POINT('Ctrl Pts',(23.2631303530518,13.410349443299,10.9061179932801));
#129516=CARTESIAN_POINT('Ctrl Pts',(23.2561980920098,13.2942369915247,10.9980296115055));
#129517=CARTESIAN_POINT('Ctrl Pts',(23.2492662073036,13.1781308432153,11.089936240071));
#129518=CARTESIAN_POINT('Ctrl Pts',(23.2423343225974,13.0580200053115,11.1767804876996));
#129519=CARTESIAN_POINT('Ctrl Pts',(23.2354024378912,12.9343681645872,11.2582291600247));
#129520=CARTESIAN_POINT('Ctrl Pts',(23.2284690113988,12.8106888212853,11.3396959481209));
#129521=CARTESIAN_POINT('Ctrl Pts',(23.2215355849065,12.6834671776639,11.4157645810553));
#129522=CARTESIAN_POINT('Ctrl Pts',(23.2146021584141,12.5531954963905,11.4861454658511));
#129523=CARTESIAN_POINT('Ctrl Pts',(23.2104832091711,12.4758048377378,11.5279567250416));
#129524=CARTESIAN_POINT('Ctrl Pts',(23.2063642599281,12.3973382765711,11.5677615089315));
#129525=CARTESIAN_POINT('Ctrl Pts',(23.2022453106851,12.3179031154636,11.6055067912478));
#129526=CARTESIAN_POINT('Ctrl Pts',(23.1953326016546,12.1845894660025,11.6688535669748));
#129527=CARTESIAN_POINT('Ctrl Pts',(23.1884198926241,12.0484976489229,11.7264202163307));
#129528=CARTESIAN_POINT('Ctrl Pts',(23.1815071835936,11.9101480240635,11.7779800768106));
#129529=CARTESIAN_POINT('Ctrl Pts',(23.1744104595967,11.7681155591704,11.8309124507215));
#129530=CARTESIAN_POINT('Ctrl Pts',(23.1673137355999,11.6237037330732,11.8775136140333));
#129531=CARTESIAN_POINT('Ctrl Pts',(23.1602170116031,11.4774963192628,11.9175915775158));
#129532=CARTESIAN_POINT('Ctrl Pts',(23.1533056473611,11.3351077055635,11.9566227422935));
#129533=CARTESIAN_POINT('Ctrl Pts',(23.1463942831192,11.1910164761425,11.9894671487316));
#129534=CARTESIAN_POINT('Ctrl Pts',(23.1394829188772,11.045776141037,12.0159983087484));
#129535=CARTESIAN_POINT('Ctrl Pts',(23.132293515003,10.8946928828906,12.0435967998619));
#129536=CARTESIAN_POINT('Ctrl Pts',(23.1251041111287,10.7423665149036,12.0643634254656));
#129537=CARTESIAN_POINT('Ctrl Pts',(23.1179147072544,10.5894305429874,12.0782147350843));
#129538=CARTESIAN_POINT('Ctrl Pts',(23.1107253033801,10.4364945710712,12.092066044703));
#129539=CARTESIAN_POINT('Ctrl Pts',(23.1035358995059,10.2829494015725,12.0990020099706));
#129540=CARTESIAN_POINT('Ctrl Pts',(23.0963464956316,10.1294332248244,12.0989999995628));
#129541=CARTESIAN_POINT('',(23.2216535038391,10.1293865181645,12.0989501584294));
#129542=CARTESIAN_POINT('Ctrl Pts',(23.4778327564119,14.6092485246315,9.43417544670676));
#129543=CARTESIAN_POINT('Ctrl Pts',(23.4577732893052,14.4047091522646,9.81069483620949));
#129544=CARTESIAN_POINT('Ctrl Pts',(23.3989319405624,13.6670015456634,10.8402272996134));
#129545=CARTESIAN_POINT('Ctrl Pts',(23.3135388565479,12.092423032665,11.8658595382605));
#129546=CARTESIAN_POINT('Ctrl Pts',(23.2482052396401,10.6965329474454,12.0983697707759));
#129547=CARTESIAN_POINT('Ctrl Pts',(23.2216535043684,10.1293865324873,12.0988146186003));
#129548=CARTESIAN_POINT('Ctrl Pts',(23.2216535036445,10.1293865128977,12.0989999987371));
#129549=CARTESIAN_POINT('Ctrl Pts',(23.2144616473686,9.97576251488196,12.0989965795681));
#129550=CARTESIAN_POINT('Ctrl Pts',(23.2072697910928,9.82216920243597,12.0920461851236));
#129551=CARTESIAN_POINT('Ctrl Pts',(23.2000779348169,9.66922023943467,12.0781830945737));
#129552=CARTESIAN_POINT('Ctrl Pts',(23.1950396449697,9.56207110048146,12.0684712391514));
#129553=CARTESIAN_POINT('Ctrl Pts',(23.1900013551225,9.45523816700231,12.0553678804514));
#129554=CARTESIAN_POINT('Ctrl Pts',(23.1849630652753,9.34893090479854,12.0388999680105));
#129555=CARTESIAN_POINT('Ctrl Pts',(23.1780322106042,9.20269077031505,12.0162461089975));
#129556=CARTESIAN_POINT('Ctrl Pts',(23.1711013559331,9.05741147522505,11.9872176032497));
#129557=CARTESIAN_POINT('Ctrl Pts',(23.1641705012619,8.91365350675345,11.9519206682721));
#129558=CARTESIAN_POINT('Ctrl Pts',(23.1572409972287,8.76992355285804,11.9166306117213));
#129559=CARTESIAN_POINT('Ctrl Pts',(23.1503114931954,8.6277146554914,11.8750746419589));
#129560=CARTESIAN_POINT('Ctrl Pts',(23.1433819891621,8.48757530416641,11.8274096877323));
#129561=CARTESIAN_POINT('Ctrl Pts',(23.1364522650283,8.34743150162177,11.7797432195329));
#129562=CARTESIAN_POINT('Ctrl Pts',(23.1295225408946,8.20935769125029,11.7259674819089));
#129563=CARTESIAN_POINT('Ctrl Pts',(23.1225928167608,8.07388595843718,11.6662888800555));
#129564=CARTESIAN_POINT('Ctrl Pts',(23.1156634748197,7.93842169724982,11.6066135696355));
#129565=CARTESIAN_POINT('Ctrl Pts',(23.1087341328786,7.80555952912581,11.5410361807239));
#129566=CARTESIAN_POINT('Ctrl Pts',(23.1018047909375,7.67581036564082,11.4698107541862));
#129567=CARTESIAN_POINT('Ctrl Pts',(23.0948738940547,7.54603208649339,11.3985693446901));
#129568=CARTESIAN_POINT('Ctrl Pts',(23.0879429971719,7.4193684981623,11.321677524493));
#129569=CARTESIAN_POINT('Ctrl Pts',(23.0810121002891,7.29630531956496,11.2394349744694));
#129570=CARTESIAN_POINT('Ctrl Pts',(23.0768805403151,7.22294642942954,11.1904095693044));
#129571=CARTESIAN_POINT('Ctrl Pts',(23.0727489803412,7.15086641510118,11.139483671144));
#129572=CARTESIAN_POINT('Ctrl Pts',(23.0686174203672,7.08016321996373,11.0867280557823));
#129573=CARTESIAN_POINT('Ctrl Pts',(23.0616832524995,6.96149912529913,10.9981861260548));
#129574=CARTESIAN_POINT('Ctrl Pts',(23.0547490846318,6.84667369731443,10.9044571565873));
#129575=CARTESIAN_POINT('Ctrl Pts',(23.0478149167641,6.73613270977454,10.805897979929));
#129576=CARTESIAN_POINT('Ctrl Pts',(23.0408820598754,6.62561262119616,10.7073574369422));
#129577=CARTESIAN_POINT('Ctrl Pts',(23.0339492029866,6.51937560346518,10.603988728551));
#129578=CARTESIAN_POINT('Ctrl Pts',(23.0270163460979,6.4178330651246,10.4961878617364));
#129579=CARTESIAN_POINT('Ctrl Pts',(23.0200832422255,6.3162869093225,10.3883831545067));
#129580=CARTESIAN_POINT('Ctrl Pts',(23.0131501383532,6.21943579656273,10.2761462111623));
#129581=CARTESIAN_POINT('Ctrl Pts',(23.0062170344808,6.127653461249,10.159909062028));
#129582=CARTESIAN_POINT('Ctrl Pts',(22.9992843056565,6.0358760909238,10.0436782007715));
#129583=CARTESIAN_POINT('Ctrl Pts',(22.9923515768321,5.94916715343914,9.92344782666485));
#129584=CARTESIAN_POINT('Ctrl Pts',(22.9854188480078,5.86785936094203,9.79968213615932));
#129585=CARTESIAN_POINT('Ctrl Pts',(22.9784845828,5.78653354957469,9.67588901755805));
#129586=CARTESIAN_POINT('Ctrl Pts',(22.9715503175923,5.71061145639965,9.54855929336527));
#129587=CARTESIAN_POINT('Ctrl Pts',(22.9646160523846,5.64038215784226,9.41818568336285));
#129588=CARTESIAN_POINT('Ctrl Pts',(22.9605012934094,5.59870843641641,9.34082262241638));
#129589=CARTESIAN_POINT('Ctrl Pts',(22.9563865344342,5.55903840082034,9.26238827233416));
#129590=CARTESIAN_POINT('Ctrl Pts',(22.952271775459,5.52142478724157,9.18298965493686));
#129591=CARTESIAN_POINT('Ctrl Pts',(22.9453381235802,5.45804326136591,9.04919752373096));
#129592=CARTESIAN_POINT('Ctrl Pts',(22.9384044717014,5.40048158569252,8.91262014426123));
#129593=CARTESIAN_POINT('Ctrl Pts',(22.9314708198227,5.34896652564976,8.77378146923933));
#129594=CARTESIAN_POINT('Ctrl Pts',(22.9245384819542,5.29746122832944,8.63496910581344));
#129595=CARTESIAN_POINT('Ctrl Pts',(22.9176061440857,5.25200037531062,8.49389661159093));
#129596=CARTESIAN_POINT('Ctrl Pts',(22.9106738062172,5.21276202370896,8.3511064623106));
#129597=CARTESIAN_POINT('Ctrl Pts',(22.9037412208191,5.17352227104248,8.20831121449157));
#129598=CARTESIAN_POINT('Ctrl Pts',(22.896808635421,5.14050555518979,8.06379850674376));
#129599=CARTESIAN_POINT('Ctrl Pts',(22.8898760500228,5.1138397764683,7.9181250035164));
#129600=CARTESIAN_POINT('Ctrl Pts',(22.8829438381066,5.08717543432276,7.77245934821475));
#129601=CARTESIAN_POINT('Ctrl Pts',(22.8760116261904,5.06686140326674,7.62563334790481));
#129602=CARTESIAN_POINT('Ctrl Pts',(22.8690794142742,5.05297427438577,7.4782128785143));
#129603=CARTESIAN_POINT('Ctrl Pts',(22.8621456590075,5.03908405374907,7.33075958822291));
#129604=CARTESIAN_POINT('Ctrl Pts',(22.8552119037409,5.03162362532709,7.18271189362287));
#129605=CARTESIAN_POINT('Ctrl Pts',(22.8482781484743,5.03061766757055,7.03464043935698));
#129606=CARTESIAN_POINT('Ctrl Pts',(22.8441608091664,5.03002031891117,6.94671399898356));
#129607=CARTESIAN_POINT('Ctrl Pts',(22.8400434698586,5.03169789774968,6.85877924044733));
#129608=CARTESIAN_POINT('Ctrl Pts',(22.8359261305508,5.03564687217782,6.77095565456406));
#129609=CARTESIAN_POINT('Ctrl Pts',(22.8289927902407,5.04229669662495,6.62306626225003));
#129610=CARTESIAN_POINT('Ctrl Pts',(22.8220594499305,5.05539250041431,6.475441072363));
#129611=CARTESIAN_POINT('Ctrl Pts',(22.8151261096204,5.07488932497261,6.32864917971366));
#129612=CARTESIAN_POINT('Ctrl Pts',(22.8081940896352,5.09438243672551,6.1818852408334));
#129613=CARTESIAN_POINT('Ctrl Pts',(22.80126206965,5.12027409374897,6.03595461015652));
#129614=CARTESIAN_POINT('Ctrl Pts',(22.7943300496648,5.15246762548975,5.89141994286524));
#129615=CARTESIAN_POINT('Ctrl Pts',(22.7873977885484,5.18466227708647,5.74688024791794));
#129616=CARTESIAN_POINT('Ctrl Pts',(22.7804655274321,5.22315917345089,5.60373693696147));
#129617=CARTESIAN_POINT('Ctrl Pts',(22.7735332663157,5.26781068180806,5.46254171654044));
#129618=CARTESIAN_POINT('Ctrl Pts',(22.7666013815341,5.31245976614917,5.32135416124642));
#129619=CARTESIAN_POINT('Ctrl Pts',(22.7596694967524,5.3632626933397,5.18211479983415));
#129620=CARTESIAN_POINT('Ctrl Pts',(22.7527376119707,5.42002218067565,5.04535945266349));
#129621=CARTESIAN_POINT('Ctrl Pts',(22.745804185402,5.4767942924346,4.90857368842192));
#129622=CARTESIAN_POINT('Ctrl Pts',(22.7388707588332,5.53952548479153,4.77427334785503));
#129623=CARTESIAN_POINT('Ctrl Pts',(22.7319373322644,5.60797037248141,4.64297415638445));
#129624=CARTESIAN_POINT('Ctrl Pts',(22.7278183833905,5.64863150738803,4.56497309132748));
#129625=CARTESIAN_POINT('Ctrl Pts',(22.7236994345165,5.69130821780815,4.48803078158937));
#129626=CARTESIAN_POINT('Ctrl Pts',(22.7195804856426,5.73594135530312,4.41225128043519));
#129627=CARTESIAN_POINT('Ctrl Pts',(22.712646772094,5.81107542461016,4.28468636765235));
#129628=CARTESIAN_POINT('Ctrl Pts',(22.7057130585453,5.89178185117034,4.16037392365949));
#129629=CARTESIAN_POINT('Ctrl Pts',(22.6987793449967,5.97775435333472,4.03979576964767));
#129630=CARTESIAN_POINT('Ctrl Pts',(22.6918469457557,6.0637105591351,3.91924047161232));
#129631=CARTESIAN_POINT('Ctrl Pts',(22.6849145465148,6.15493065717947,3.80241832029139));
#129632=CARTESIAN_POINT('Ctrl Pts',(22.6779821472738,6.25106569159728,3.68978122846771));
#129633=CARTESIAN_POINT('Ctrl Pts',(22.6710495015589,6.34720414399177,3.57714013195465));
#129634=CARTESIAN_POINT('Ctrl Pts',(22.664116855844,6.44825767038205,3.46868464626526));
#129635=CARTESIAN_POINT('Ctrl Pts',(22.6571842101292,6.55383741425312,3.36483314373467));
#129636=CARTESIAN_POINT('Ctrl Pts',(22.6502519386425,6.65941145886836,3.26098724716845));
#129637=CARTESIAN_POINT('Ctrl Pts',(22.6433196671559,6.76951099574575,3.16174506759461));
#129638=CARTESIAN_POINT('Ctrl Pts',(22.6363873956692,6.8837107393556,3.0674876890866));
#129639=CARTESIAN_POINT('Ctrl Pts',(22.6294535825151,6.99793587984121,2.97320934868449));
#129640=CARTESIAN_POINT('Ctrl Pts',(22.6225197693609,7.11626279402301,2.8839182349048));
#129641=CARTESIAN_POINT('Ctrl Pts',(22.6155859562067,7.23823310513727,2.79995514992151));
#129642=CARTESIAN_POINT('Ctrl Pts',(22.6114689177159,7.31065450652515,2.75010101555235));
#129643=CARTESIAN_POINT('Ctrl Pts',(22.6073518792252,7.38435979545037,2.70212451134012));
#129644=CARTESIAN_POINT('Ctrl Pts',(22.6032348407344,7.45924813015834,2.65608978550349));
#129645=CARTESIAN_POINT('Ctrl Pts',(22.5963013558529,7.58536721737681,2.57856292333585));
#129646=CARTESIAN_POINT('Ctrl Pts',(22.5893678709714,7.71488667542895,2.50651889974949));
#129647=CARTESIAN_POINT('Ctrl Pts',(22.5824343860899,7.84731029346206,2.44024001252563));
#129648=CARTESIAN_POINT('Ctrl Pts',(22.5755022191216,7.97970874048388,2.37397372355761));
#129649=CARTESIAN_POINT('Ctrl Pts',(22.5685700521532,8.11500995065018,2.31347053248644));
#129650=CARTESIAN_POINT('Ctrl Pts',(22.5616378851848,8.2526940110444,2.25896632791747));
#129651=CARTESIAN_POINT('Ctrl Pts',(22.5547054748914,8.39038290426868,2.20446021020359));
#129652=CARTESIAN_POINT('Ctrl Pts',(22.547773064598,8.53045450894213,2.15595362514326));
#129653=CARTESIAN_POINT('Ctrl Pts',(22.5408406543045,8.67236936204863,2.11363414141517));
#129654=CARTESIAN_POINT('Ctrl Pts',(22.5339086194588,8.81427652928533,2.07131694963916));
#129655=CARTESIAN_POINT('Ctrl Pts',(22.526976584613,8.95802642811843,2.03518628227907));
#129656=CARTESIAN_POINT('Ctrl Pts',(22.5200445497673,9.10306486807957,2.00537970212355));
#129657=CARTESIAN_POINT('Ctrl Pts',(22.5131109730705,9.2481355680739,1.97556649226858));
#129658=CARTESIAN_POINT('Ctrl Pts',(22.5061773963736,9.39449505792165,1.95208024682282));
#129659=CARTESIAN_POINT('Ctrl Pts',(22.4992438196768,9.54157877108378,1.9350074404211));
#129660=CARTESIAN_POINT('Ctrl Pts',(22.4951256117266,9.62893935615771,1.92486702226029));
#129661=CARTESIAN_POINT('Ctrl Pts',(22.4910074037764,9.7165552643328,1.91698814636579));
#129662=CARTESIAN_POINT('Ctrl Pts',(22.4868891958262,9.80430724843803,1.9113802780782));
#129663=CARTESIAN_POINT('Ctrl Pts',(22.4799556232921,9.95204984768639,1.90193865638155));
#129664=CARTESIAN_POINT('Ctrl Pts',(22.4730220507579,10.1002293919555,1.89893406231333));
#129665=CARTESIAN_POINT('Ctrl Pts',(22.4660884782238,10.2482752299219,1.90238355260451));
#129666=CARTESIAN_POINT('Ctrl Pts',(22.4591562219442,10.3962929631829,1.90583238805183));
#129667=CARTESIAN_POINT('Ctrl Pts',(22.4522239656647,10.5441767104752,1.91573285564485));
#129668=CARTESIAN_POINT('Ctrl Pts',(22.4452917093852,10.6913566113617,1.93204990669116));
#129669=CARTESIAN_POINT('Ctrl Pts',(22.4383592081633,10.838541712659,1.94836753427928));
#129670=CARTESIAN_POINT('Ctrl Pts',(22.4314267069415,10.9850225888615,1.9711021658943));
#129671=CARTESIAN_POINT('Ctrl Pts',(22.4244942057197,11.1302347335151,2.00016690347203));
#129672=CARTESIAN_POINT('Ctrl Pts',(22.4175620792479,11.2754390284404,2.02923006989818));
#129673=CARTESIAN_POINT('Ctrl Pts',(22.410629952776,11.4193744050801,2.06462259177438));
#129674=CARTESIAN_POINT('Ctrl Pts',(22.4036978263042,11.5614867616133,2.10620649040397));
#129675=CARTESIAN_POINT('Ctrl Pts',(22.3967641577058,11.7036307325799,2.14779963982234));
#129676=CARTESIAN_POINT('Ctrl Pts',(22.3898304891073,11.8439505557084,2.19558682522712));
#129677=CARTESIAN_POINT('Ctrl Pts',(22.3828968205088,11.9819068852309,2.24938006871217));
#129678=CARTESIAN_POINT('Ctrl Pts',(22.3787790639786,12.063836179762,2.28132671809408));
#129679=CARTESIAN_POINT('Ctrl Pts',(22.3746613074483,12.1449322010469,2.31539070984882));
#129680=CARTESIAN_POINT('Ctrl Pts',(22.370543550918,12.2250851901569,2.35152458210273));
#129681=CARTESIAN_POINT('Ctrl Pts',(22.3636099924989,12.3600483499194,2.41236749798139));
#129682=CARTESIAN_POINT('Ctrl Pts',(22.3566764340798,12.4923832519696,2.47910262136328));
#129683=CARTESIAN_POINT('Ctrl Pts',(22.3497428756607,12.6215776949439,2.55147780017193));
#129684=CARTESIAN_POINT('Ctrl Pts',(22.3428106341768,12.7507475991896,2.62383923229903));
#129685=CARTESIAN_POINT('Ctrl Pts',(22.3358783926929,12.8767779461898,2.7018384210654));
#129686=CARTESIAN_POINT('Ctrl Pts',(22.328946151209,12.9991816332476,2.78517754539985));
#129687=CARTESIAN_POINT('Ctrl Pts',(22.3220136656563,13.1215896298659,2.86851960391878));
#129688=CARTESIAN_POINT('Ctrl Pts',(22.3150811801037,13.2403704359038,2.95720179093612));
#129689=CARTESIAN_POINT('Ctrl Pts',(22.308148694551,13.3550659593708,3.0508829794816));
#129690=CARTESIAN_POINT('Ctrl Pts',(22.3012165842048,13.4697552751808,3.14455909772731));
#129691=CARTESIAN_POINT('Ctrl Pts',(22.2942844738585,13.580359495408,3.24323346626158));
#129692=CARTESIAN_POINT('Ctrl Pts',(22.2873523635122,13.6864536413925,3.34652469654105));
#129693=CARTESIAN_POINT('Ctrl Pts',(22.2804187116004,13.7925713806377,3.44983889676766));
#129694=CARTESIAN_POINT('Ctrl Pts',(22.2734850596885,13.8941768046595,3.55777177953251));
#129695=CARTESIAN_POINT('Ctrl Pts',(22.2665514077766,13.9908813866036,3.66990468797189));
#129696=CARTESIAN_POINT('Ctrl Pts',(22.2624335738543,14.0483133738203,3.73649942045101));
#129697=CARTESIAN_POINT('Ctrl Pts',(22.2583157399321,14.1040175187899,3.80457484120395));
#129698=CARTESIAN_POINT('Ctrl Pts',(22.2541979060098,14.1579190618731,3.874037610281));
#129699=CARTESIAN_POINT('Ctrl Pts',(22.2472642956059,14.248678501657,3.99099904861213));
#129700=CARTESIAN_POINT('Ctrl Pts',(22.240330685202,14.3343563570106,4.11193599116586));
#129701=CARTESIAN_POINT('Ctrl Pts',(22.2333970747981,14.4146181346602,4.23638577728254));
#129702=CARTESIAN_POINT('Ctrl Pts',(22.2264647807023,14.4948646750486,4.36081193728546));
#129703=CARTESIAN_POINT('Ctrl Pts',(22.2195324866065,14.569697010104,4.48874933264206));
#129704=CARTESIAN_POINT('Ctrl Pts',(22.2126001925108,14.6388242094336,4.61970670416093));
#129705=CARTESIAN_POINT('Ctrl Pts',(22.2056676539223,14.7079538467869,4.75066869437094));
#129706=CARTESIAN_POINT('Ctrl Pts',(22.1987351153338,14.7713777885139,4.88465058310104));
#129707=CARTESIAN_POINT('Ctrl Pts',(22.1918025767453,14.8288510170149,5.0211364324741));
#129708=CARTESIAN_POINT('Ctrl Pts',(22.1848704132515,14.8863211358465,5.1576148970895));
#129709=CARTESIAN_POINT('Ctrl Pts',(22.1779382497577,14.9378410582831,5.29659674622179));
#129710=CARTESIAN_POINT('Ctrl Pts',(22.1710060862639,14.9832138788456,5.43754597433969));
#129711=CARTESIAN_POINT('Ctrl Pts',(22.1640723815,15.028596787423,5.57852654055607));
#129712=CARTESIAN_POINT('Ctrl Pts',(22.1571386767362,15.0678297619024,5.72147504499835));
#129713=CARTESIAN_POINT('Ctrl Pts',(22.1502049719723,15.1007655570025,5.86583962255727));
#129714=CARTESIAN_POINT('Ctrl Pts',(22.1460874016821,15.1203244300737,5.95157031282543));
#129715=CARTESIAN_POINT('Ctrl Pts',(22.1419698313918,15.1376635206223,6.03780011735071));
#129716=CARTESIAN_POINT('Ctrl Pts',(22.1378522611016,15.1527604864707,6.12441157781638));
#129717=CARTESIAN_POINT('Ctrl Pts',(22.1309189472056,15.1781813040225,6.2702510899736));
#129718=CARTESIAN_POINT('Ctrl Pts',(22.1239856333095,15.1972510326479,6.41722360612239));
#129719=CARTESIAN_POINT('Ctrl Pts',(22.1170523194135,15.2098907721861,6.56476374015232));
#129720=CARTESIAN_POINT('Ctrl Pts',(22.1101203233419,15.2225281092719,6.71227583102898));
#129721=CARTESIAN_POINT('Ctrl Pts',(22.1031883272702,15.2287378674464,6.86035499529251));
#129722=CARTESIAN_POINT('Ctrl Pts',(22.0962563311985,15.2284930298674,7.00843097644207));
#129723=CARTESIAN_POINT('Ctrl Pts',(22.089324090006,15.2282481836308,7.15651219367546));
#129724=CARTESIAN_POINT('Ctrl Pts',(22.0823918488135,15.2215482821267,7.30458989694481));
#129725=CARTESIAN_POINT('Ctrl Pts',(22.075459607621,15.2084184326879,7.45209352362437));
#129726=CARTESIAN_POINT('Ctrl Pts',(22.0685277404533,15.195289291662,7.59958919183696));
#129727=CARTESIAN_POINT('Ctrl Pts',(22.0615958732855,15.1757309271479,7.74651051618775));
#129728=CARTESIAN_POINT('Ctrl Pts',(22.0546640061178,15.1498203546764,7.89229173279906));
#129729=CARTESIAN_POINT('Ctrl Pts',(22.0477305934374,15.1239040052451,8.03810545244515));
#129730=CARTESIAN_POINT('Ctrl Pts',(22.0407971807569,15.0916326758373,8.18277823079145));
#129731=CARTESIAN_POINT('Ctrl Pts',(22.0338637680765,15.0531346874517,8.3257535459212));
#129732=CARTESIAN_POINT('Ctrl Pts',(22.0297447174488,15.030263531423,8.41069332791269));
#129733=CARTESIAN_POINT('Ctrl Pts',(22.0256256668211,15.0051957146653,8.49503421516281));
#129734=CARTESIAN_POINT('Ctrl Pts',(22.0215066161934,14.9779665423999,8.57866183434857));
#129735=CARTESIAN_POINT('Ctrl Pts',(22.0142262297089,14.9298392150951,8.72647293051569));
#129736=CARTESIAN_POINT('Ctrl Pts',(22.0069458432244,14.8749389088111,8.87210820366851));
#129737=CARTESIAN_POINT('Ctrl Pts',(21.99966545674,14.8134928711808,9.01494709179358));
#129738=CARTESIAN_POINT('Ctrl Pts',(21.9923850702555,14.7520468335505,9.15778597991866));
#129739=CARTESIAN_POINT('Ctrl Pts',(21.985104683771,14.6840552228045,9.29782809214351));
#129740=CARTESIAN_POINT('Ctrl Pts',(21.9778242972865,14.6098038194187,9.43447708670711));
#129741=CARTESIAN_POINT('Origin',(26.8463464956315,10.1295,7.));
#129742=CARTESIAN_POINT('',(20.352563293369,14.6098038194187,9.43447708670712));
#129743=CARTESIAN_POINT('',(20.4776000250576,14.6098038194187,9.43447708670711));
#129744=CARTESIAN_POINT('',(26.8463464956315,14.6098038194187,9.43447708670711));
#129745=CARTESIAN_POINT('',(21.5963464956316,10.1298829051514,12.098999985623));
#129746=CARTESIAN_POINT('Ctrl Pts',(21.5963464956316,10.1298829051514,12.098999985623));
#129747=CARTESIAN_POINT('Ctrl Pts',(21.5886997577445,9.96656989073889,12.0990122494776));
#129748=CARTESIAN_POINT('Ctrl Pts',(21.5810530198574,9.80325714346398,12.0911738586918));
#129749=CARTESIAN_POINT('Ctrl Pts',(21.5734062819704,9.64065518488774,12.0755129540508));
#129750=CARTESIAN_POINT('Ctrl Pts',(21.5666845761133,9.49772331596717,12.0617465616352));
#129751=CARTESIAN_POINT('Ctrl Pts',(21.5599628702561,9.35531775886811,12.0419328173513));
#129752=CARTESIAN_POINT('Ctrl Pts',(21.553241164399,9.21397363696974,12.0161352133487));
#129753=CARTESIAN_POINT('Ctrl Pts',(21.5465211079346,9.07266419852288,11.9903439396408));
#129754=CARTESIAN_POINT('Ctrl Pts',(21.5398010514701,8.93241603785332,11.9585717981774));
#129755=CARTESIAN_POINT('Ctrl Pts',(21.5330809950056,8.79375579412643,11.9209336935662));
#129756=CARTESIAN_POINT('Ctrl Pts',(21.5263596207543,8.65506835945939,11.8832882082133));
#129757=CARTESIAN_POINT('Ctrl Pts',(21.5196382465029,8.51796982061406,11.8397745520151));
#129758=CARTESIAN_POINT('Ctrl Pts',(21.5129168722516,8.38297363001403,11.790558071764));
#129759=CARTESIAN_POINT('Ctrl Pts',(21.5061950124626,8.24796768757988,11.7413380362204));
#129760=CARTESIAN_POINT('Ctrl Pts',(21.4994731526736,8.11506473991455,11.6864144868448));
#129761=CARTESIAN_POINT('Ctrl Pts',(21.4927512928847,7.9847596072539,11.6260014751104));
#129762=CARTESIAN_POINT('Ctrl Pts',(21.4860249738077,7.85436803004691,11.5655483853277));
#129763=CARTESIAN_POINT('Ctrl Pts',(21.4792986547307,7.72657804372845,11.4995987153755));
#129764=CARTESIAN_POINT('Ctrl Pts',(21.4725723356537,7.60186164562879,11.4284134122179));
#129765=CARTESIAN_POINT('Ctrl Pts',(21.4674017694565,7.50599132118198,11.3736927963763));
#129766=CARTESIAN_POINT('Ctrl Pts',(21.4622312032594,7.41193676657903,11.3158793604137));
#129767=CARTESIAN_POINT('Ctrl Pts',(21.4570606370622,7.31990104245665,11.2551092462793));
#129768=CARTESIAN_POINT('Ctrl Pts',(21.4497821926166,7.19034522990356,11.1695650557955));
#129769=CARTESIAN_POINT('Ctrl Pts',(21.4425037481711,7.06471083663906,11.0781083746355));
#129770=CARTESIAN_POINT('Ctrl Pts',(21.4352253037255,6.94350501939066,10.9811100190188));
#129771=CARTESIAN_POINT('Ctrl Pts',(21.4279477400291,6.82231386900175,10.8841234009679));
#129772=CARTESIAN_POINT('Ctrl Pts',(21.4206701763327,6.70555042157178,10.7815966068709));
#129773=CARTESIAN_POINT('Ctrl Pts',(21.4133926126363,6.59368928068819,10.6739411477594));
#129774=CARTESIAN_POINT('Ctrl Pts',(21.4061193938006,6.48189492329082,10.5663499612524));
#129775=CARTESIAN_POINT('Ctrl Pts',(21.3988461749649,6.374997207616,10.4536364025609));
#129776=CARTESIAN_POINT('Ctrl Pts',(21.3915729561292,6.27343466828419,10.3362495646368));
#129777=CARTESIAN_POINT('Ctrl Pts',(21.3843045826288,6.17193978875607,10.2189409284834));
#129778=CARTESIAN_POINT('Ctrl Pts',(21.3770362091284,6.07577315665127,10.0969654188858));
#129779=CARTESIAN_POINT('Ctrl Pts',(21.369767835628,5.98533451912964,9.97080687140086));
#129780=CARTESIAN_POINT('Ctrl Pts',(21.362508451111,5.89500772938303,9.84480434741678));
#129781=CARTESIAN_POINT('Ctrl Pts',(21.3552490665939,5.81039493847136,9.71462931976104));
#129782=CARTESIAN_POINT('Ctrl Pts',(21.3479896820768,5.73185403598033,9.58079657763674));
#129783=CARTESIAN_POINT('Ctrl Pts',(21.3455647854359,5.70561853761555,9.53609160766829));
#129784=CARTESIAN_POINT('Ctrl Pts',(21.3431398887949,5.68006019676905,9.49097876732916));
#129785=CARTESIAN_POINT('Ctrl Pts',(21.340714992154,5.65519129922816,9.44547800035033));
#129786=CARTESIAN_POINT('Ctrl Pts',(21.3339842151457,5.58616278850139,9.31918168277893));
#129787=CARTESIAN_POINT('Ctrl Pts',(21.3272534381374,5.5224727999895,9.18993727191009));
#129788=CARTESIAN_POINT('Ctrl Pts',(21.320522661129,5.46436371111823,9.05822846306196));
#129789=CARTESIAN_POINT('Ctrl Pts',(21.3137921028903,5.4062565109596,8.92652393512921));
#129790=CARTESIAN_POINT('Ctrl Pts',(21.3070615446516,5.35372999568264,8.79235550376603));
#129791=CARTESIAN_POINT('Ctrl Pts',(21.300330986413,5.30697886832858,8.65622792350045));
#129792=CARTESIAN_POINT('Ctrl Pts',(21.2935969859559,5.26020383098292,8.52003072332438));
#129793=CARTESIAN_POINT('Ctrl Pts',(21.2868629854988,5.21921020433078,8.38187271779147));
#129794=CARTESIAN_POINT('Ctrl Pts',(21.2801289850417,5.18414331691862,8.24227544333062));
#129795=CARTESIAN_POINT('Ctrl Pts',(21.2733933187736,5.14906775489957,8.10264363625035));
#129796=CARTESIAN_POINT('Ctrl Pts',(21.2666576525055,5.11992193614123,7.96157220729983));
#129797=CARTESIAN_POINT('Ctrl Pts',(21.2599219862374,5.09680022375923,7.81959377878687));
#129798=CARTESIAN_POINT('Ctrl Pts',(21.2531800695621,5.07365705542761,7.67748360042942));
#129799=CARTESIAN_POINT('Ctrl Pts',(21.2464381528869,5.05654921504801,7.53446510332673));
#129800=CARTESIAN_POINT('Ctrl Pts',(21.2396962362117,5.04551934956642,7.39107767261366));
#129801=CARTESIAN_POINT('Ctrl Pts',(21.234587273223,5.03716101806671,7.28241998492099));
#129802=CARTESIAN_POINT('Ctrl Pts',(21.2294783102344,5.03229187939357,7.17355058473459));
#129803=CARTESIAN_POINT('Ctrl Pts',(21.2243693472458,5.03091055206464,7.06470426108234));
#129804=CARTESIAN_POINT('Ctrl Pts',(21.2176534134252,5.0290947426829,6.92162146563229));
#129805=CARTESIAN_POINT('Ctrl Pts',(21.2109374796046,5.03330466935425,6.77833298901328));
#129806=CARTESIAN_POINT('Ctrl Pts',(21.204221545784,5.04355373597305,6.63537471367122));
#129807=CARTESIAN_POINT('Ctrl Pts',(21.1975109705907,5.05379462488651,6.49253050438969));
#129808=CARTESIAN_POINT('Ctrl Pts',(21.1908003953973,5.0700650298353,6.35001633899631));
#129809=CARTESIAN_POINT('Ctrl Pts',(21.184089820204,5.092326300591,6.20836743246488));
#129810=CARTESIAN_POINT('Ctrl Pts',(21.177383231775,5.1145743458873,6.06680267979342));
#129811=CARTESIAN_POINT('Ctrl Pts',(21.170676643346,5.14280610952076,5.92610252631899));
#129812=CARTESIAN_POINT('Ctrl Pts',(21.163970054917,5.17693118965687,5.78679631602257));
#129813=CARTESIAN_POINT('Ctrl Pts',(21.1572660848589,5.21104294675723,5.64754449333819));
#129814=CARTESIAN_POINT('Ctrl Pts',(21.1505621148008,5.25104334803021,5.50968588807691));
#129815=CARTESIAN_POINT('Ctrl Pts',(21.1438581447427,5.29679107030568,5.37373882760094));
#129816=CARTESIAN_POINT('Ctrl Pts',(21.1371541064382,5.3425392582927,5.23779038318468));
#129817=CARTESIAN_POINT('Ctrl Pts',(21.1304500681338,5.39403477490237,5.10375387565751));
#129818=CARTESIAN_POINT('Ctrl Pts',(21.1237460298293,5.45108660716885,4.9721318766305));
#129819=CARTESIAN_POINT('Ctrl Pts',(21.1170416407376,5.50814142465893,4.8405029905136));
#129820=CARTESIAN_POINT('Ctrl Pts',(21.1103372516459,5.57075299036046,4.7112892041865));
#129821=CARTESIAN_POINT('Ctrl Pts',(21.1036328625542,5.63868250959758,4.58497220142382));
#129822=CARTESIAN_POINT('Ctrl Pts',(21.0969268835225,5.70662813826123,4.45862524269358));
#129823=CARTESIAN_POINT('Ctrl Pts',(21.0902209044908,5.77989405761444,4.33517676178452));
#129824=CARTESIAN_POINT('Ctrl Pts',(21.083514925459,5.85819603824447,4.21508286186258));
#129825=CARTESIAN_POINT('Ctrl Pts',(21.0768061164871,5.9365310625094,4.09493828200956));
#129826=CARTESIAN_POINT('Ctrl Pts',(21.0700973075152,6.01990617971834,3.97815141278116));
#129827=CARTESIAN_POINT('Ctrl Pts',(21.0633884985432,6.10799454326904,3.86514835096091));
#129828=CARTESIAN_POINT('Ctrl Pts',(21.0566717408833,6.19618727510909,3.75201140157848));
#129829=CARTESIAN_POINT('Ctrl Pts',(21.0499549832234,6.28910418051396,3.64266750672083));
#129830=CARTESIAN_POINT('Ctrl Pts',(21.0432382255635,6.38637840804699,3.53750931440167));
#129831=CARTESIAN_POINT('Ctrl Pts',(21.0365170846755,6.48371611488792,3.43228249784938));
#129832=CARTESIAN_POINT('Ctrl Pts',(21.0297959437875,6.58541655150024,3.33124709056119));
#129833=CARTESIAN_POINT('Ctrl Pts',(21.0230748028994,6.69107726063957,3.23475763523128));
#129834=CARTESIAN_POINT('Ctrl Pts',(21.0163437401092,6.79689394853999,3.13812573995541));
#129835=CARTESIAN_POINT('Ctrl Pts',(21.0096126773189,6.90668230663511,3.04605344237268));
#129836=CARTESIAN_POINT('Ctrl Pts',(21.0028816145286,7.02000750204106,2.95885444395564));
#129837=CARTESIAN_POINT('Ctrl Pts',(20.9991470954955,7.08288243165579,2.91047481515106));
#129838=CARTESIAN_POINT('Ctrl Pts',(20.9954125764625,7.14684556635783,2.86359453102167));
#129839=CARTESIAN_POINT('Ctrl Pts',(20.9916780574294,7.21181912996737,2.81826120607161));
#129840=CARTESIAN_POINT('Ctrl Pts',(20.9851848545906,7.32478857099484,2.73944021958085));
#129841=CARTESIAN_POINT('Ctrl Pts',(20.9786916517519,7.44117320825419,2.66504792986056));
#129842=CARTESIAN_POINT('Ctrl Pts',(20.9721984489131,7.5605842685465,2.59540320066743));
#129843=CARTESIAN_POINT('Ctrl Pts',(20.9657137060064,7.67983974930792,2.52584921092733));
#129844=CARTESIAN_POINT('Ctrl Pts',(20.9592289630997,7.80211347051053,2.46103068201201));
#129845=CARTESIAN_POINT('Ctrl Pts',(20.9527442201929,7.92698482267687,2.40122539216573));
#129846=CARTESIAN_POINT('Ctrl Pts',(20.9462662847788,8.05172508856619,2.34148288415577));
#129847=CARTESIAN_POINT('Ctrl Pts',(20.9397883493646,8.17905720344274,2.28674332075701));
#129848=CARTESIAN_POINT('Ctrl Pts',(20.9333104139505,8.30853331594534,2.23724015558595));
#129849=CARTESIAN_POINT('Ctrl Pts',(20.9268376417297,8.4379062304142,2.18777644656792));
#129850=CARTESIAN_POINT('Ctrl Pts',(20.9203648695088,8.56941937043855,2.14354097624593));
#129851=CARTESIAN_POINT('Ctrl Pts',(20.913892097288,8.70260256867763,2.10472015912414));
#129852=CARTESIAN_POINT('Ctrl Pts',(20.9074222385477,8.83572581939468,2.06591681576646));
#129853=CARTESIAN_POINT('Ctrl Pts',(20.9009523798074,8.97051725008775,2.0325233937257));
#129854=CARTESIAN_POINT('Ctrl Pts',(20.8944825210671,9.10648943525271,2.00467714913086));
#129855=CARTESIAN_POINT('Ctrl Pts',(20.8880140950404,9.24243151014611,1.97683707092942));
#129856=CARTESIAN_POINT('Ctrl Pts',(20.8815456690137,9.37955342700358,1.95454180910562));
#129857=CARTESIAN_POINT('Ctrl Pts',(20.8750772429871,9.51735593402644,1.93787785187938));
#129858=CARTESIAN_POINT('Ctrl Pts',(20.8686087712671,9.65515941449231,1.9212137769382));
#129859=CARTESIAN_POINT('Ctrl Pts',(20.8621402995472,9.79364309633967,1.91018113416146));
#129860=CARTESIAN_POINT('Ctrl Pts',(20.8556718278273,9.93230148100156,1.90481465066237));
#129861=CARTESIAN_POINT('Ctrl Pts',(20.8492018320787,10.0709925347955,1.89944690277268));
#129862=CARTESIAN_POINT('Ctrl Pts',(20.8427318363301,10.2098579723973,1.89974798431359));
#129863=CARTESIAN_POINT('Ctrl Pts',(20.8362618405815,10.348391704133,1.90570049743228));
#129864=CARTESIAN_POINT('Ctrl Pts',(20.8297845845163,10.4870808917277,1.91165969017352));
#129865=CARTESIAN_POINT('Ctrl Pts',(20.8233073284511,10.6254372286438,1.92328296238145));
#129866=CARTESIAN_POINT('Ctrl Pts',(20.8168300723859,10.7629587075596,1.94050090761774));
#129867=CARTESIAN_POINT('Ctrl Pts',(20.8103491685813,10.9005576332404,1.95772854933322));
#129868=CARTESIAN_POINT('Ctrl Pts',(20.8038682647766,11.0373203698811,1.98055707009204));
#129869=CARTESIAN_POINT('Ctrl Pts',(20.797387360972,11.1727557922092,2.00886602543851));
#129870=CARTESIAN_POINT('Ctrl Pts',(20.7908954455442,11.3084213311811,2.03722308017937));
#129871=CARTESIAN_POINT('Ctrl Pts',(20.7844035301164,11.4427546621861,2.07107907258841));
#129872=CARTESIAN_POINT('Ctrl Pts',(20.7779116146886,11.5752797124002,2.1102636039136));
#129873=CARTESIAN_POINT('Ctrl Pts',(20.77160333233,11.704056102916,2.14833974499001));
#129874=CARTESIAN_POINT('Ctrl Pts',(20.7652950499715,11.8311248479618,2.1914468562064));
#129875=CARTESIAN_POINT('Ctrl Pts',(20.758986767613,11.956069933585,2.23938624989138));
#129876=CARTESIAN_POINT('Ctrl Pts',(20.752255350081,12.089395852133,2.29054123262481));
#129877=CARTESIAN_POINT('Ctrl Pts',(20.7455239325489,12.2207429681633,2.34736702175228));
#129878=CARTESIAN_POINT('Ctrl Pts',(20.7387925150168,12.3496051713782,2.40969129273208));
#129879=CARTESIAN_POINT('Ctrl Pts',(20.7320693455013,12.4783094795322,2.47193919768429));
#129880=CARTESIAN_POINT('Ctrl Pts',(20.7253461759858,12.604534607748,2.53967200821282));
#129881=CARTESIAN_POINT('Ctrl Pts',(20.7186230064702,12.7277927942082,2.61266874335141));
#129882=CARTESIAN_POINT('Ctrl Pts',(20.7119067023597,12.8509251148298,2.68559093743474));
#129883=CARTESIAN_POINT('Ctrl Pts',(20.7051903982492,12.9710962113983,2.7637661629336));
#129884=CARTESIAN_POINT('Ctrl Pts',(20.6984740941386,13.0878414666366,2.84692682862695));
#129885=CARTESIAN_POINT('Ctrl Pts',(20.691763278558,13.2044913182398,2.93001953584278));
#129886=CARTESIAN_POINT('Ctrl Pts',(20.6850524629774,13.3177206051619,3.01808935397584));
#129887=CARTESIAN_POINT('Ctrl Pts',(20.6783416473968,13.427092417135,3.11082460533681));
#129888=CARTESIAN_POINT('Ctrl Pts',(20.6716350714244,13.5363951326426,3.20350127050457));
#129889=CARTESIAN_POINT('Ctrl Pts',(20.6649284954521,13.6418449478012,3.30083725726319));
#129890=CARTESIAN_POINT('Ctrl Pts',(20.6582219194797,13.7430369628603,3.40247979602026));
#129891=CARTESIAN_POINT('Ctrl Pts',(20.6515176619563,13.8441939960568,3.50408719716967));
#129892=CARTESIAN_POINT('Ctrl Pts',(20.6448134044329,13.9410958999718,3.60999792371146));
#129893=CARTESIAN_POINT('Ctrl Pts',(20.6381091469095,14.0333736471028,3.71982141531038));
#129894=CARTESIAN_POINT('Ctrl Pts',(20.6314059678938,14.1256365495977,3.82962723970549));
#129895=CARTESIAN_POINT('Ctrl Pts',(20.6247027888781,14.2132765396375,3.94334429217381));
#129896=CARTESIAN_POINT('Ctrl Pts',(20.6179996098624,14.2959640876569,4.060548009192));
#129897=CARTESIAN_POINT('Ctrl Pts',(20.6112962704155,14.378653614687,4.17775453131697));
#129898=CARTESIAN_POINT('Ctrl Pts',(20.6045929309686,14.456390251492,4.29844758149486));
#129899=CARTESIAN_POINT('Ctrl Pts',(20.5978895915217,14.5288871829675,4.42217273380445));
#129900=CARTESIAN_POINT('Ctrl Pts',(20.5911823410669,14.6014264121778,4.54597007253031));
#129901=CARTESIAN_POINT('Ctrl Pts',(20.5844750906121,14.668719640705,4.67280272880459));
#129902=CARTESIAN_POINT('Ctrl Pts',(20.5777678401573,14.7305252782473,4.80219032013015));
#129903=CARTESIAN_POINT('Ctrl Pts',(20.5710585028671,14.7923501454557,4.93161816798048));
#129904=CARTESIAN_POINT('Ctrl Pts',(20.564349165577,14.8486838674656,5.06360219779874));
#129905=CARTESIAN_POINT('Ctrl Pts',(20.5576398282869,14.8993327590442,5.19764142004176));
#129906=CARTESIAN_POINT('Ctrl Pts',(20.5509240694714,14.9500301268172,5.33180893159575));
#129907=CARTESIAN_POINT('Ctrl Pts',(20.544208310656,14.9950316728671,5.4680352158438));
#129908=CARTESIAN_POINT('Ctrl Pts',(20.5374925518406,15.0341932052633,5.60580289691735));
#129909=CARTESIAN_POINT('Ctrl Pts',(20.5337601938259,15.055957664548,5.68236882531709));
#129910=CARTESIAN_POINT('Ctrl Pts',(20.5300278358113,15.0759192163065,5.75941061027489));
#129911=CARTESIAN_POINT('Ctrl Pts',(20.5262954777967,15.0940599329618,5.83683807144917));
#129912=CARTESIAN_POINT('Ctrl Pts',(20.5195531565522,15.1268302456745,5.97670697318204));
#129913=CARTESIAN_POINT('Ctrl Pts',(20.5128108353077,15.1537122172889,6.11807599491532));
#129914=CARTESIAN_POINT('Ctrl Pts',(20.5060685140632,15.174579088646,6.26042039691011));
#129915=CARTESIAN_POINT('Ctrl Pts',(20.4993310938359,15.1954307918007,6.40266132825656));
#129916=CARTESIAN_POINT('Ctrl Pts',(20.4925936736085,15.210276051231,6.54587586687352));
#129917=CARTESIAN_POINT('Ctrl Pts',(20.4858562533812,15.2190391491384,6.68952898784726));
#129918=CARTESIAN_POINT('Ctrl Pts',(20.4791225787158,15.2277973753404,6.83310224714431));
#129919=CARTESIAN_POINT('Ctrl Pts',(20.4723889040505,15.2304801549966,6.97711323862747));
#129920=CARTESIAN_POINT('Ctrl Pts',(20.4656552293852,15.2270636067672,7.12102179540484));
#129921=CARTESIAN_POINT('Ctrl Pts',(20.4589238948687,15.2236482458881,7.26488033975022));
#129922=CARTESIAN_POINT('Ctrl Pts',(20.4521925603523,15.2141377896593,7.40863615508474));
#129923=CARTESIAN_POINT('Ctrl Pts',(20.4454612258358,15.1985604617482,7.5517490689985));
#129924=CARTESIAN_POINT('Ctrl Pts',(20.4387300007792,15.1829833871439,7.69485965571826));
#129925=CARTESIAN_POINT('Ctrl Pts',(20.4319987757226,15.1613396706609,7.83732699762378));
#129926=CARTESIAN_POINT('Ctrl Pts',(20.425267550666,15.1337094284331,7.97861585741374));
#129927=CARTESIAN_POINT('Ctrl Pts',(20.4201616447402,15.1127507743489,8.08578916099432));
#129928=CARTESIAN_POINT('Ctrl Pts',(20.4150557388143,15.0883486417902,8.19228444747359));
#129929=CARTESIAN_POINT('Ctrl Pts',(20.4099498328885,15.0605576408463,8.2978719284471));
#129930=CARTESIAN_POINT('Ctrl Pts',(20.4026905362803,15.0210459220998,8.44799040959878));
#129931=CARTESIAN_POINT('Ctrl Pts',(20.3954312396722,14.9746971733673,8.59621860003053));
#129932=CARTESIAN_POINT('Ctrl Pts',(20.3881719430641,14.9217188865059,8.74196416260962));
#129933=CARTESIAN_POINT('Ctrl Pts',(20.3809028745946,14.868669284681,8.88790591574319));
#129934=CARTESIAN_POINT('Ctrl Pts',(20.3736338061251,14.8089723919441,9.03135812139184));
#129935=CARTESIAN_POINT('Ctrl Pts',(20.3663647376557,14.7428843972005,9.17174708556652));
#129936=CARTESIAN_POINT('Ctrl Pts',(20.3617642562268,14.7010583236443,9.26059709780911));
#129937=CARTESIAN_POINT('Ctrl Pts',(20.3571637747979,14.6566732928353,9.34822058344851));
#129938=CARTESIAN_POINT('Ctrl Pts',(20.352563293369,14.6098038194187,9.43447708670712));
#129939=CARTESIAN_POINT('Ctrl Pts',(21.8525208814298,14.6095924811794,9.43436249769606));
#129940=CARTESIAN_POINT('Ctrl Pts',(21.8370464448822,14.4519305706909,9.72490119905027));
#129941=CARTESIAN_POINT('Ctrl Pts',(21.7827901266984,13.8010022388993,10.6901681055195));
#129942=CARTESIAN_POINT('Ctrl Pts',(21.6973986661381,12.2874582761103,11.804511236185));
#129943=CARTESIAN_POINT('Ctrl Pts',(21.6274816421253,10.7948600303933,12.0984964626806));
#129944=CARTESIAN_POINT('Ctrl Pts',(21.5963464997487,10.1298830029783,12.0991317633798));
#129945=CARTESIAN_POINT('',(21.7216535043236,10.1294562983577,12.0989999998127));
#129946=CARTESIAN_POINT('Ctrl Pts',(21.9778242972865,14.6098038194187,9.43447708670711));
#129947=CARTESIAN_POINT('Ctrl Pts',(21.9708912000632,14.5390943591803,9.5646076459575));
#129948=CARTESIAN_POINT('Ctrl Pts',(21.9639581028398,14.462708632086,9.69166097956588));
#129949=CARTESIAN_POINT('Ctrl Pts',(21.9570250056164,14.3809405674658,9.81514726103373));
#129950=CARTESIAN_POINT('Ctrl Pts',(21.9500922255905,14.2991762438321,9.9386278928569));
#129951=CARTESIAN_POINT('Ctrl Pts',(21.9431594455646,14.2120302589396,10.0585415242968));
#129952=CARTESIAN_POINT('Ctrl Pts',(21.9362266655387,14.1198398936231,10.1744272764327));
#129953=CARTESIAN_POINT('Ctrl Pts',(21.9292924040556,14.0276298282607,10.2903377920526));
#129954=CARTESIAN_POINT('Ctrl Pts',(21.9223581425725,13.9303734348502,10.4022184502355));
#129955=CARTESIAN_POINT('Ctrl Pts',(21.9154238810893,13.8284486805062,10.5096409586995));
#129956=CARTESIAN_POINT('Ctrl Pts',(21.9120029111546,13.7781648080188,10.5626371101512));
#129957=CARTESIAN_POINT('Ctrl Pts',(21.9085819412199,13.7267453168927,10.6145487329785));
#129958=CARTESIAN_POINT('Ctrl Pts',(21.9051609712852,13.6742389692849,10.6653276305991));
#129959=CARTESIAN_POINT('Ctrl Pts',(21.8982288511239,13.5678421526517,10.7682240098965));
#129960=CARTESIAN_POINT('Ctrl Pts',(21.8912967309625,13.4569435049872,10.8665024520393));
#129961=CARTESIAN_POINT('Ctrl Pts',(21.8843646108012,13.3419664401948,10.959780343734));
#129962=CARTESIAN_POINT('Ctrl Pts',(21.877433811209,13.2270112785383,11.0530404659862));
#129963=CARTESIAN_POINT('Ctrl Pts',(21.8705030116169,13.1079795066484,11.1413017300309));
#129964=CARTESIAN_POINT('Ctrl Pts',(21.8635722120248,12.9853276996924,11.2242217211777));
#129965=CARTESIAN_POINT('Ctrl Pts',(21.8566411598445,12.8626714227769,11.3071447342857));
#129966=CARTESIAN_POINT('Ctrl Pts',(21.8497101076642,12.7363951190217,11.3847258969099));
#129967=CARTESIAN_POINT('Ctrl Pts',(21.8427790554839,12.6069848824144,11.4566657556304));
#129968=CARTESIAN_POINT('Ctrl Pts',(21.8358483702673,12.4775814974174,11.5286018055031));
#129969=CARTESIAN_POINT('Ctrl Pts',(21.8289176850508,12.3450448012554,11.5948969892324));
#129970=CARTESIAN_POINT('Ctrl Pts',(21.8219869998343,12.209886058069,11.6552975038543));
#129971=CARTESIAN_POINT('Ctrl Pts',(21.8150547479171,12.0746967618723,11.7157116721808));
#129972=CARTESIAN_POINT('Ctrl Pts',(21.8081224959998,11.9368845365065,11.7702283738594));
#129973=CARTESIAN_POINT('Ctrl Pts',(21.8011902440826,11.7969818008886,11.8186414520802));
#129974=CARTESIAN_POINT('Ctrl Pts',(21.7970652715141,11.713733968355,11.847449207771));
#129975=CARTESIAN_POINT('Ctrl Pts',(21.7929402989456,11.6297463168938,11.8740967543871));
#129976=CARTESIAN_POINT('Ctrl Pts',(21.788815326377,11.5451338329821,11.8985489536103));
#129977=CARTESIAN_POINT('Ctrl Pts',(21.781841763805,11.4020903481749,11.939887153677));
#129978=CARTESIAN_POINT('Ctrl Pts',(21.7748682012329,11.2572131443299,11.9749619273583));
#129979=CARTESIAN_POINT('Ctrl Pts',(21.7678946386609,11.1110621236963,12.0036323603283));
#129980=CARTESIAN_POINT('Ctrl Pts',(21.7609226052006,10.9649431499895,12.0322965066555));
#129981=CARTESIAN_POINT('Ctrl Pts',(21.7539505717403,10.8175512332713,12.0545590528571));
#129982=CARTESIAN_POINT('Ctrl Pts',(21.7469785382801,10.669456698842,12.0703301434301));
#129983=CARTESIAN_POINT('Ctrl Pts',(21.7400073493926,10.5213801041739,12.0860993235369));
#129984=CARTESIAN_POINT('Ctrl Pts',(21.7330361605051,10.3726013821705,12.0953785825651));
#129985=CARTESIAN_POINT('Ctrl Pts',(21.7260649716176,10.2236966737367,12.0981298518826));
#129986=CARTESIAN_POINT('Ctrl Pts',(21.7245944825346,10.192287002918,12.0987101993042));
#129987=CARTESIAN_POINT('Ctrl Pts',(21.7231239934515,10.1608717378449,12.0990002690569));
#129988=CARTESIAN_POINT('Ctrl Pts',(21.7216535043684,10.1294562993151,12.0989999998127));
#129989=CARTESIAN_POINT('Ctrl Pts',(21.7216535043236,10.1294562983577,12.0989999998127));
#129990=CARTESIAN_POINT('Ctrl Pts',(21.7145780823896,9.97829741836422,12.0989987042859));
#129991=CARTESIAN_POINT('Ctrl Pts',(21.7075026604556,9.8271603213621,12.092271455827));
#129992=CARTESIAN_POINT('Ctrl Pts',(21.7004272385216,9.67663880551781,12.0788500409573));
#129993=CARTESIAN_POINT('Ctrl Pts',(21.6933497400828,9.52607311440785,12.065424687152));
#129994=CARTESIAN_POINT('Ctrl Pts',(21.686272241644,9.37612366434497,12.0453012699465));
#129995=CARTESIAN_POINT('Ctrl Pts',(21.6791947432053,9.22737926268248,12.0185634573353));
#129996=CARTESIAN_POINT('Ctrl Pts',(21.6769530559598,9.18026679336472,12.0100946722101));
#129997=CARTESIAN_POINT('Ctrl Pts',(21.6747113687143,9.13327515566229,12.0009627140914));
#129998=CARTESIAN_POINT('Ctrl Pts',(21.6724696814689,9.08642286948864,11.9911713154133));
#129999=CARTESIAN_POINT('Ctrl Pts',(21.6655384929631,8.94155786744673,11.960896784428));
#130000=CARTESIAN_POINT('Ctrl Pts',(21.6586073044574,8.79798658804774,11.9243058365266));
#130001=CARTESIAN_POINT('Ctrl Pts',(21.6516761159517,8.65626323121066,11.8815340235511));
#130002=CARTESIAN_POINT('Ctrl Pts',(21.64474624141,8.51456674125142,11.8387703189433));
#130003=CARTESIAN_POINT('Ctrl Pts',(21.6378163668684,8.37471779167141,11.7898281825944));
#130004=CARTESIAN_POINT('Ctrl Pts',(21.6308864923267,8.2372559332038,11.7348931763742));
#130005=CARTESIAN_POINT('Ctrl Pts',(21.6239563464653,8.09978869280394,11.6799560193284));
#130006=CARTESIAN_POINT('Ctrl Pts',(21.6170262006039,7.9647090391401,11.6190256426999));
#130007=CARTESIAN_POINT('Ctrl Pts',(21.6100960547425,7.83253754293167,11.5523361552964));
#130008=CARTESIAN_POINT('Ctrl Pts',(21.6031662631196,7.70037280274875,11.4856500767661));
#130009=CARTESIAN_POINT('Ctrl Pts',(21.5962364714968,7.57111621763294,11.4132056266103));
#130010=CARTESIAN_POINT('Ctrl Pts',(21.5893066798739,7.44526470784607,11.3352833697874));
#130011=CARTESIAN_POINT('Ctrl Pts',(21.5823752942246,7.31938424904482,11.2573431888844));
#130012=CARTESIAN_POINT('Ctrl Pts',(21.5754439085753,7.19691071214243,11.1739228579809));
#130013=CARTESIAN_POINT('Ctrl Pts',(21.568512522926,7.07831346210215,11.0853471958881));
#130014=CARTESIAN_POINT('Ctrl Pts',(21.5643830274709,7.00765705517126,11.0325766803587));
#130015=CARTESIAN_POINT('Ctrl Pts',(21.5602535320158,6.9383759408189,10.9779771655619));
#130016=CARTESIAN_POINT('Ctrl Pts',(21.5561240365606,6.87056406102977,10.9216243504048));
#130017=CARTESIAN_POINT('Ctrl Pts',(21.5491919803161,6.75673035668187,10.8270266232852));
#130018=CARTESIAN_POINT('Ctrl Pts',(21.5422599240716,6.64699821171827,10.7274524655712));
#130019=CARTESIAN_POINT('Ctrl Pts',(21.5353278678271,6.54179397638852,10.6232811770744));
#130020=CARTESIAN_POINT('Ctrl Pts',(21.5283971552673,6.43661013346749,10.5191300807637));
#130021=CARTESIAN_POINT('Ctrl Pts',(21.5214664427075,6.33595268411619,10.4103838641845));
#130022=CARTESIAN_POINT('Ctrl Pts',(21.5145357301477,6.24021162379281,10.297459162249));
#130023=CARTESIAN_POINT('Ctrl Pts',(21.5076047985457,6.14446753761436,10.1845308913768));
#130024=CARTESIAN_POINT('Ctrl Pts',(21.5006738669437,6.05364036800616,10.0674241210261));
#130025=CARTESIAN_POINT('Ctrl Pts',(21.4937429353417,5.96808061140313,9.94658949842187));
#130026=CARTESIAN_POINT('Ctrl Pts',(21.4868123893406,5.88252561489794,9.82576159842469));
#130027=CARTESIAN_POINT('Ctrl Pts',(21.4798818433394,5.80223763552051,9.7012065317229));
#130028=CARTESIAN_POINT('Ctrl Pts',(21.4729512973382,5.72752452675666,9.57340492984763));
#130029=CARTESIAN_POINT('Ctrl Pts',(21.4660192119694,5.65279482320388,9.44557494151323));
#130030=CARTESIAN_POINT('Ctrl Pts',(21.4590871266005,5.58364263152974,9.31449726290405));
#130031=CARTESIAN_POINT('Ctrl Pts',(21.4521550412316,5.5203307404732,9.18067873310885));
#130032=CARTESIAN_POINT('Ctrl Pts',(21.4480294913719,5.48265140599206,9.10103819387072));
#130033=CARTESIAN_POINT('Ctrl Pts',(21.4439039415122,5.44703976938654,9.02042734711839));
#130034=CARTESIAN_POINT('Ctrl Pts',(21.4397783916525,5.41354327869334,8.93895673050291));
#130035=CARTESIAN_POINT('Ctrl Pts',(21.4328288078177,5.35711766800913,8.8017175988741));
#130036=CARTESIAN_POINT('Ctrl Pts',(21.425879223983,5.3066782204933,8.66199295346232));
#130037=CARTESIAN_POINT('Ctrl Pts',(21.4189296401482,5.26242423305924,8.52032051846249));
#130038=CARTESIAN_POINT('Ctrl Pts',(21.4119812825149,5.21817805390603,8.37867308049059));
#130039=CARTESIAN_POINT('Ctrl Pts',(21.4050329248816,5.18011525469409,8.23507885105442));
#130040=CARTESIAN_POINT('Ctrl Pts',(21.3980845672483,5.14838550186882,8.09009144410335));
#130041=CARTESIAN_POINT('Ctrl Pts',(21.3911359899612,5.11665474599245,7.94509945376403));
#130042=CARTESIAN_POINT('Ctrl Pts',(21.3841874126742,5.09125751019233,7.79871451694216));
#130043=CARTESIAN_POINT('Ctrl Pts',(21.3772388353872,5.07229262147526,7.6515017502624));
#130044=CARTESIAN_POINT('Ctrl Pts',(21.3702906875388,5.05332890483344,7.50429808168186));
#130045=CARTESIAN_POINT('Ctrl Pts',(21.3633425396903,5.04079678109596,7.35626701042103));
#130046=CARTESIAN_POINT('Ctrl Pts',(21.3563943918419,5.03474335699634,7.20798016388597));
#130047=CARTESIAN_POINT('Ctrl Pts',(21.3494449282258,5.02868878656242,7.05966523633523));
#130048=CARTESIAN_POINT('Ctrl Pts',(21.3424954646096,5.02911538076994,6.91109476395886));
#130049=CARTESIAN_POINT('Ctrl Pts',(21.3355460009934,5.03601815715149,6.76284242248547));
#130050=CARTESIAN_POINT('Ctrl Pts',(21.331508249577,5.04002878252507,6.67670540028748));
#130051=CARTESIAN_POINT('Ctrl Pts',(21.3274704981606,5.04622466346145,6.59067577933083));
#130052=CARTESIAN_POINT('Ctrl Pts',(21.3234327467442,5.0545967490254,6.50486568161013));
#130053=CARTESIAN_POINT('Ctrl Pts',(21.31655060643,5.06886653971637,6.35860676866734));
#130054=CARTESIAN_POINT('Ctrl Pts',(21.3096684661157,5.08946675265018,6.21293115702204));
#130055=CARTESIAN_POINT('Ctrl Pts',(21.3027863258014,5.11632565505071,6.06839708719742));
#130056=CARTESIAN_POINT('Ctrl Pts',(21.2959056901371,5.14317868525947,5.92389461701757));
#130057=CARTESIAN_POINT('Ctrl Pts',(21.2890250544729,5.17628761360455,5.78053352530322));
#130058=CARTESIAN_POINT('Ctrl Pts',(21.2821444188086,5.21552937377503,5.63886309116306));
#130059=CARTESIAN_POINT('Ctrl Pts',(21.2752633519625,5.25477359306887,5.49718377910633));
#130060=CARTESIAN_POINT('Ctrl Pts',(21.2683822851165,5.30015132574767,5.35719566559861));
#130061=CARTESIAN_POINT('Ctrl Pts',(21.2615012182705,5.35148915214393,5.21943454549694));
#130062=CARTESIAN_POINT('Ctrl Pts',(21.2546203142567,5.4028257636912,5.08167668534937));
#130063=CARTESIAN_POINT('Ctrl Pts',(21.247739410243,5.46012206546334,4.946146031246));
#130064=CARTESIAN_POINT('Ctrl Pts',(21.2408585062293,5.52315589001064,4.81335989692717));
#130065=CARTESIAN_POINT('Ctrl Pts',(21.2339753023867,5.58621078257564,4.68052938102991));
#130066=CARTESIAN_POINT('Ctrl Pts',(21.2270920985441,5.65500688289976,4.55044552515016));
#130067=CARTESIAN_POINT('Ctrl Pts',(21.2202088947016,5.72927504815719,4.42360302492416));
#130068=CARTESIAN_POINT('Ctrl Pts',(21.2158349637464,5.7764687437722,4.34300097523082));
#130069=CARTESIAN_POINT('Ctrl Pts',(21.2114610327912,5.82587110691438,4.26370729362511));
#130070=CARTESIAN_POINT('Ctrl Pts',(21.2070871018361,5.87740373338063,4.1858432276432));
#130071=CARTESIAN_POINT('Ctrl Pts',(21.2000240344735,5.96061913294572,4.060107556734));
#130072=CARTESIAN_POINT('Ctrl Pts',(21.1929609671109,6.04941838500955,3.93806054204195));
#130073=CARTESIAN_POINT('Ctrl Pts',(21.1858978997482,6.14345469960175,3.820181787716));
#130074=CARTESIAN_POINT('Ctrl Pts',(21.178835666965,6.23747990276482,3.70231696206676));
#130075=CARTESIAN_POINT('Ctrl Pts',(21.1717734341818,6.33674074326747,3.58861965076045));
#130076=CARTESIAN_POINT('Ctrl Pts',(21.1647112013986,6.44084960845913,3.4795370632564));
#130077=CARTESIAN_POINT('Ctrl Pts',(21.1576495020065,6.54495061059453,3.37046271446018));
#130078=CARTESIAN_POINT('Ctrl Pts',(21.1505878026143,6.65389869778801,3.26600261454694));
#130079=CARTESIAN_POINT('Ctrl Pts',(21.1435261032221,6.76726836629837,3.16656819007615));
#130080=CARTESIAN_POINT('Ctrl Pts',(21.1364656539791,6.88061796471118,3.06715136871406));
#130081=CARTESIAN_POINT('Ctrl Pts',(21.129405204736,6.99838735271096,2.97275864623127));
#130082=CARTESIAN_POINT('Ctrl Pts',(21.122344755493,7.12011654019953,2.88376237422092));
#130083=CARTESIAN_POINT('Ctrl Pts',(21.1152853450695,7.24182781740339,2.794779196429));
#130084=CARTESIAN_POINT('Ctrl Pts',(21.108225934646,7.36749748609508,2.71119106380588));
#130085=CARTESIAN_POINT('Ctrl Pts',(21.1011665242225,7.4966345737675,2.6333284246065));
#130086=CARTESIAN_POINT('Ctrl Pts',(21.097691501791,7.56020281098323,2.5950002354853));
#130087=CARTESIAN_POINT('Ctrl Pts',(21.0942164793594,7.62461079760845,2.55805875715));
#130088=CARTESIAN_POINT('Ctrl Pts',(21.0907414569279,7.68979747601854,2.52253949269471));
#130089=CARTESIAN_POINT('Ctrl Pts',(21.0840196099996,7.81589015100785,2.45383344449506));
#130090=CARTESIAN_POINT('Ctrl Pts',(21.0772977630712,7.9449362626361,2.39043095335399));
#130091=CARTESIAN_POINT('Ctrl Pts',(21.0705759161429,8.07645702253597,2.33257934907452));
#130092=CARTESIAN_POINT('Ctrl Pts',(21.0638557183066,8.20794551603063,2.27474193771263));
#130093=CARTESIAN_POINT('Ctrl Pts',(21.0571355204702,8.34190711156151,2.22245284749552));
#130094=CARTESIAN_POINT('Ctrl Pts',(21.0504153226339,8.47784123377184,2.17591207377585));
#130095=CARTESIAN_POINT('Ctrl Pts',(21.0436938073277,8.61380200536455,2.12936217590945));
#130096=CARTESIAN_POINT('Ctrl Pts',(21.0369722920214,8.75173573007874,2.08856297103887));
#130097=CARTESIAN_POINT('Ctrl Pts',(21.0302507767151,8.89112448377531,2.05366528823461));
#130098=CARTESIAN_POINT('Ctrl Pts',(21.0235287760831,9.03052330201039,2.01876508564978));
#130099=CARTESIAN_POINT('Ctrl Pts',(21.0168067754511,9.17137700030015,1.98976733838324));
#130100=CARTESIAN_POINT('Ctrl Pts',(21.0100847748191,9.31315578902763,1.96677209643634));
#130101=CARTESIAN_POINT('Ctrl Pts',(21.0033583161372,9.45502860584993,1.94376160397975));
#130102=CARTESIAN_POINT('Ctrl Pts',(20.9966318574553,9.59782737480171,1.92676162587731));
#130103=CARTESIAN_POINT('Ctrl Pts',(20.9899053987734,9.74101492534841,1.91582058275154));
#130104=CARTESIAN_POINT('Ctrl Pts',(20.9847355365222,9.85106687800675,1.90741144972626));
#130105=CARTESIAN_POINT('Ctrl Pts',(20.9795656742709,9.96134831898086,1.90258042790854));
#130106=CARTESIAN_POINT('Ctrl Pts',(20.9743958120197,10.071614880693,1.90132857373974));
#130107=CARTESIAN_POINT('Ctrl Pts',(20.9671175717702,10.2268504534471,1.89956618724759));
#130108=CARTESIAN_POINT('Ctrl Pts',(20.9598393315207,10.38215201505,1.90489782475772));
#130109=CARTESIAN_POINT('Ctrl Pts',(20.9525610912711,10.5368917561104,1.91730062299045));
#130110=CARTESIAN_POINT('Ctrl Pts',(20.9452837330259,10.6916127452311,1.92970191820577));
#130111=CARTESIAN_POINT('Ctrl Pts',(20.9380063747807,10.8457717972154,1.94917264147978));
#130112=CARTESIAN_POINT('Ctrl Pts',(20.9307290165355,10.998745255065,1.97563798213674));
#130113=CARTESIAN_POINT('Ctrl Pts',(20.9234560005045,11.1516274375505,2.00208753159934));
#130114=CARTESIAN_POINT('Ctrl Pts',(20.9161829844736,11.3033251896582,2.03552331724142));
#130115=CARTESIAN_POINT('Ctrl Pts',(20.9089099684426,11.4532236629269,2.07581918851396));
#130116=CARTESIAN_POINT('Ctrl Pts',(20.9016417943633,11.6030223424974,2.11608823313558));
#130117=CARTESIAN_POINT('Ctrl Pts',(20.894373620284,11.7510238897501,2.16320818147162));
#130118=CARTESIAN_POINT('Ctrl Pts',(20.8871054462047,11.8966261080614,2.21700237108486));
#130119=CARTESIAN_POINT('Ctrl Pts',(20.8798462532636,12.0420484086068,2.27073008828768));
#130120=CARTESIAN_POINT('Ctrl Pts',(20.8725870603225,12.1850770620086,2.33111549332836));
#130121=CARTESIAN_POINT('Ctrl Pts',(20.8653278673814,12.3251271892484,2.39793282906112));
#130122=CARTESIAN_POINT('Ctrl Pts',(20.8629019672915,12.3719295843671,2.42026205795495));
#130123=CARTESIAN_POINT('Ctrl Pts',(20.8604760672015,12.4183994834494,2.44330918750438));
#130124=CARTESIAN_POINT('Ctrl Pts',(20.8580501671115,12.4645155072712,2.46706457350171));
#130125=CARTESIAN_POINT('Ctrl Pts',(20.851319308004,12.5924682041796,2.53297584365391));
#130126=CARTESIAN_POINT('Ctrl Pts',(20.8445884488965,12.7176517637429,2.60432077926021));
#130127=CARTESIAN_POINT('Ctrl Pts',(20.8378575897889,12.8395943566171,2.68083462018041));
#130128=CARTESIAN_POINT('Ctrl Pts',(20.8311269491109,12.9615329922165,2.75734597807738));
#130129=CARTESIAN_POINT('Ctrl Pts',(20.8243963084329,13.0802305615075,2.8390257118703));
#130130=CARTESIAN_POINT('Ctrl Pts',(20.8176656677548,13.1952429162414,2.92556490154576));
#130131=CARTESIAN_POINT('Ctrl Pts',(20.8109315848184,13.3103140918602,3.01214835004661));
#130132=CARTESIAN_POINT('Ctrl Pts',(20.804197501882,13.4216959931946,3.10359600184866));
#130133=CARTESIAN_POINT('Ctrl Pts',(20.7974634189456,13.52897595819,3.19955736661001));
#130134=CARTESIAN_POINT('Ctrl Pts',(20.790727670196,13.6362824610811,3.29554246937953));
#130135=CARTESIAN_POINT('Ctrl Pts',(20.7839919214463,13.7394847375183,3.3960432610415));
#130136=CARTESIAN_POINT('Ctrl Pts',(20.7772561726966,13.8382061214154,3.5006715065636));
#130137=CARTESIAN_POINT('Ctrl Pts',(20.7705141740967,13.9370191052046,3.60539683273453));
#130138=CARTESIAN_POINT('Ctrl Pts',(20.7637721754969,14.0313426428299,3.71425699380575));
#130139=CARTESIAN_POINT('Ctrl Pts',(20.757030176897,14.1208391087228,3.82682916955609));
#130140=CARTESIAN_POINT('Ctrl Pts',(20.7519216253324,14.1886524290741,3.91212743179073));
#130141=CARTESIAN_POINT('Ctrl Pts',(20.7468130737678,14.2536951325735,3.99955619341295));
#130142=CARTESIAN_POINT('Ctrl Pts',(20.7417045222033,14.3158368081123,4.08892028122819));
#130143=CARTESIAN_POINT('Ctrl Pts',(20.7349885913884,14.3975310395132,4.20640231571828));
#130144=CARTESIAN_POINT('Ctrl Pts',(20.7282726605735,14.4743500912044,4.3274317992558));
#130145=CARTESIAN_POINT('Ctrl Pts',(20.7215567297586,14.5459825288401,4.45157243139028));
#130146=CARTESIAN_POINT('Ctrl Pts',(20.7148461574089,14.6175578128304,4.57561401496664));
#130147=CARTESIAN_POINT('Ctrl Pts',(20.7081355850593,14.6839545411525,4.70276148394193));
#130148=CARTESIAN_POINT('Ctrl Pts',(20.7014250127097,14.7449047642867,4.83254991711475));
#130149=CARTESIAN_POINT('Ctrl Pts',(20.6947184269592,14.8058187782729,4.962261245917));
#130150=CARTESIAN_POINT('Ctrl Pts',(20.6880118412087,14.8612925759747,5.09461007959434));
#130151=CARTESIAN_POINT('Ctrl Pts',(20.6813052554582,14.9111043584523,5.22910735524996));
#130152=CARTESIAN_POINT('Ctrl Pts',(20.6746012879102,14.9608966947709,5.36355212414347));
#130153=CARTESIAN_POINT('Ctrl Pts',(20.6678973203622,15.0050312919063,5.50014331759118));
#130154=CARTESIAN_POINT('Ctrl Pts',(20.6611933528142,15.0433346977241,5.63837245788636));
#130155=CARTESIAN_POINT('Ctrl Pts',(20.6544893167563,15.0816384949762,5.77660301078764));
#130156=CARTESIAN_POINT('Ctrl Pts',(20.6477852806984,15.1141108743886,5.91647119019885));
#130157=CARTESIAN_POINT('Ctrl Pts',(20.6410812446405,15.1406283667068,6.05745371870328));
#130158=CARTESIAN_POINT('Ctrl Pts',(20.6343768576303,15.1671472471998,6.19844362755812));
#130159=CARTESIAN_POINT('Ctrl Pts',(20.6276724706202,15.1877105506822,6.34054763828436));
#130160=CARTESIAN_POINT('Ctrl Pts',(20.62096808361,15.2022460867859,6.48323299350801));
#130161=CARTESIAN_POINT('Ctrl Pts',(20.6142621064915,15.2167850703453,6.62595219003299));
#130162=CARTESIAN_POINT('Ctrl Pts',(20.6075561293729,15.2252934010757,6.76925263776888));
#130163=CARTESIAN_POINT('Ctrl Pts',(20.6008501522544,15.227750853798,6.91259730125182));
#130164=CARTESIAN_POINT('Ctrl Pts',(20.5941413450238,15.2302093436348,7.0560024602372));
#130165=CARTESIAN_POINT('Ctrl Pts',(20.5874325377932,15.2266118621726,7.19945150257343));
#130166=CARTESIAN_POINT('Ctrl Pts',(20.5807237305627,15.2169902963607,7.34240835917979));
#130167=CARTESIAN_POINT('Ctrl Pts',(20.5740069743707,15.2073573303917,7.48553459888278));
#130168=CARTESIAN_POINT('Ctrl Pts',(20.5672902181786,15.1916860472491,7.62816711857723));
#130169=CARTESIAN_POINT('Ctrl Pts',(20.5605734619866,15.1700602117556,7.76977513058459));
#130170=CARTESIAN_POINT('Ctrl Pts',(20.5538523224128,15.1484202631557,7.91147555654415));
#130171=CARTESIAN_POINT('Ctrl Pts',(20.5471311828389,15.1208180850618,8.05214977921517));
#130172=CARTESIAN_POINT('Ctrl Pts',(20.5404100432651,15.0873882866751,8.19127861428358));
#130173=CARTESIAN_POINT('Ctrl Pts',(20.5336789815349,15.0539091371805,8.33061283982655));
#130174=CARTESIAN_POINT('Ctrl Pts',(20.5269479198048,15.0145852798129,8.46839676418089));
#130175=CARTESIAN_POINT('Ctrl Pts',(20.5202168580746,14.9696010262843,8.60412688256317));
#130176=CARTESIAN_POINT('Ctrl Pts',(20.5164823161787,14.9446427676627,8.6794329537237));
#130177=CARTESIAN_POINT('Ctrl Pts',(20.5127477742828,14.9179429442996,8.75410715651368));
#130178=CARTESIAN_POINT('Ctrl Pts',(20.5090132323869,14.8895392850499,8.82806646618269));
#130179=CARTESIAN_POINT('Ctrl Pts',(20.5025204017193,14.8401570167588,8.95665125311397));
#130180=CARTESIAN_POINT('Ctrl Pts',(20.4960275710517,14.7854648740825,9.08348248766354));
#130181=CARTESIAN_POINT('Ctrl Pts',(20.4895347403842,14.7256061011462,9.20807828371341));
#130182=CARTESIAN_POINT('Ctrl Pts',(20.485556501942,14.6889298833625,9.28441968409128));
#130183=CARTESIAN_POINT('Ctrl Pts',(20.4815782634998,14.6503150272754,9.35992205380894));
#130184=CARTESIAN_POINT('Ctrl Pts',(20.4776000250576,14.6098038194187,9.43447708670711));
#130185=CARTESIAN_POINT('Origin',(26.8463464956315,10.1295,7.));
#130186=CARTESIAN_POINT('',(18.8525174992326,14.6098038194187,9.43447708670712));
#130187=CARTESIAN_POINT('',(18.9778214339751,14.6099559957068,9.43455988473872));
#130188=CARTESIAN_POINT('',(26.8463464956315,14.6098038194187,9.43447708670711));
#130189=CARTESIAN_POINT('',(20.0963464956032,10.1292828156512,12.0989999953747));
#130190=CARTESIAN_POINT('Ctrl Pts',(20.0963464956032,10.1292828156512,12.0989999953747));
#130191=CARTESIAN_POINT('Ctrl Pts',(20.0890161304489,9.9727687890773,12.0989933288916));
#130192=CARTESIAN_POINT('Ctrl Pts',(20.0816857652947,9.81628384987453,12.0917760164965));
#130193=CARTESIAN_POINT('Ctrl Pts',(20.0743554001404,9.66046609801297,12.0773820221436));
#130194=CARTESIAN_POINT('Ctrl Pts',(20.0698745661482,9.56521934502955,12.0685834019081));
#130195=CARTESIAN_POINT('Ctrl Pts',(20.065393732156,9.4702218440322,12.0571042223294));
#130196=CARTESIAN_POINT('Ctrl Pts',(20.0609128981638,9.37561849205956,12.0429617956103));
#130197=CARTESIAN_POINT('Ctrl Pts',(20.0540297945509,9.23029628755551,12.0212373156105));
#130198=CARTESIAN_POINT('Ctrl Pts',(20.0471466909379,9.0858734579511,11.9932209241342));
#130199=CARTESIAN_POINT('Ctrl Pts',(20.040263587325,8.94290407468458,11.9590111020268));
#130200=CARTESIAN_POINT('Ctrl Pts',(20.0333824104595,8.79997471201355,11.9248108560777));
#130201=CARTESIAN_POINT('Ctrl Pts',(20.0265012335941,8.65849831506874,11.8844207161138));
#130202=CARTESIAN_POINT('Ctrl Pts',(20.0196200567286,8.51901756866879,11.8379900101564));
#130203=CARTESIAN_POINT('Ctrl Pts',(20.0127390888202,8.37954105780559,11.7915607141354));
#130204=CARTESIAN_POINT('Ctrl Pts',(20.0058581209118,8.24206040107134,11.7390913207874));
#130205=CARTESIAN_POINT('Ctrl Pts',(19.9989771530033,8.10710237471126,11.6807807944003));
#130206=CARTESIAN_POINT('Ctrl Pts',(19.9920967087737,7.97215461938547,11.6224747057589));
#130207=CARTESIAN_POINT('Ctrl Pts',(19.985216264544,7.83972942282541,11.5583285083938));
#130208=CARTESIAN_POINT('Ctrl Pts',(19.9783358203144,7.71033280260142,11.4885889844171));
#130209=CARTESIAN_POINT('Ctrl Pts',(19.9714536339439,7.58090341892158,11.4188318022682));
#130210=CARTESIAN_POINT('Ctrl Pts',(19.9645714475735,7.45450444365356,11.3434786251353));
#130211=CARTESIAN_POINT('Ctrl Pts',(19.957689261203,7.33161704422618,11.2628220659312));
#130212=CARTESIAN_POINT('Ctrl Pts',(19.9533152585539,7.25351543788963,11.2115604486721));
#130213=CARTESIAN_POINT('Ctrl Pts',(19.9489412559048,7.17683173753798,11.1581575511211));
#130214=CARTESIAN_POINT('Ctrl Pts',(19.9445672532557,7.10168335770222,11.1026975736245));
#130215=CARTESIAN_POINT('Ctrl Pts',(19.9376178748488,6.9822882475402,11.0145832305441));
#130216=CARTESIAN_POINT('Ctrl Pts',(19.930668496442,6.8667251055417,10.921240950437));
#130217=CARTESIAN_POINT('Ctrl Pts',(19.9237191180351,6.75544289250122,10.8230275483361));
#130218=CARTESIAN_POINT('Ctrl Pts',(19.9167708710451,6.64417879713505,10.7248301361979));
#130219=CARTESIAN_POINT('Ctrl Pts',(19.9098226240551,6.53719448530056,10.6217634011466));
#130220=CARTESIAN_POINT('Ctrl Pts',(19.9028743770652,6.43490468373816,10.5142234489366));
#130221=CARTESIAN_POINT('Ctrl Pts',(19.8959257674772,6.33260954412695,10.4066778846959));
#130222=CARTESIAN_POINT('Ctrl Pts',(19.8889771578891,6.23500963255852,10.2946588716185));
#130223=CARTESIAN_POINT('Ctrl Pts',(19.8820285483011,6.14248214411779,10.1785986876101));
#130224=CARTESIAN_POINT('Ctrl Pts',(19.8750802871826,6.04995929588631,10.0625443239643));
#130225=CARTESIAN_POINT('Ctrl Pts',(19.868132026064,5.96250856499122,9.94244945163858));
#130226=CARTESIAN_POINT('Ctrl Pts',(19.8611837649454,5.88046626630638,9.8187786947424));
#130227=CARTESIAN_POINT('Ctrl Pts',(19.8542340645085,5.79840697272408,9.6950823196972));
#130228=CARTESIAN_POINT('Ctrl Pts',(19.8472843640716,5.72175853102108,9.56780885290348));
#130229=CARTESIAN_POINT('Ctrl Pts',(19.8403346636347,5.65081375603784,9.43745164631919));
#130230=CARTESIAN_POINT('Ctrl Pts',(19.8362969785389,5.60959576928118,9.36171581354087));
#130231=CARTESIAN_POINT('Ctrl Pts',(19.8322592934432,5.57030220177107,9.28493958658977));
#130232=CARTESIAN_POINT('Ctrl Pts',(19.8282216083474,5.53298336328829,9.20722355198392));
#130233=CARTESIAN_POINT('Ctrl Pts',(19.821289621329,5.46891355651218,9.07379894599301));
#130234=CARTESIAN_POINT('Ctrl Pts',(19.8143576343105,5.41064597993131,8.93755962820844));
#130235=CARTESIAN_POINT('Ctrl Pts',(19.807425647292,5.35841008944348,8.79902808910417));
#130236=CARTESIAN_POINT('Ctrl Pts',(19.800494976297,5.30618411583254,8.66052284992904));
#130237=CARTESIAN_POINT('Ctrl Pts',(19.7935643053021,5.25998766035838,8.51972656710486));
#130238=CARTESIAN_POINT('Ctrl Pts',(19.7866336343072,5.22000157021081,8.37718051391147));
#130239=CARTESIAN_POINT('Ctrl Pts',(19.7797027024116,5.18001397481245,8.23462909466308));
#130240=CARTESIAN_POINT('Ctrl Pts',(19.772771770516,5.14623730510447,8.09032809093049));
#130241=CARTESIAN_POINT('Ctrl Pts',(19.7658408386203,5.11880232749438,7.94483323118251));
#130242=CARTESIAN_POINT('Ctrl Pts',(19.7589102686247,5.09136878240709,7.7993459684775));
#130243=CARTESIAN_POINT('Ctrl Pts',(19.7519796986291,5.07027632712535,7.65266529985237));
#130244=CARTESIAN_POINT('Ctrl Pts',(19.7450491286335,5.05560446738238,7.50535643271154));
#130245=CARTESIAN_POINT('Ctrl Pts',(19.73811698291,5.04092927185914,7.35801407356488));
#130246=CARTESIAN_POINT('Ctrl Pts',(19.7311848371864,5.03267762147763,7.21004355990087));
#130247=CARTESIAN_POINT('Ctrl Pts',(19.7242526914629,5.03087713469774,7.06201513861103));
#130248=CARTESIAN_POINT('Ctrl Pts',(19.720127115455,5.02980559850131,6.97391795662521));
#130249=CARTESIAN_POINT('Ctrl Pts',(19.7160015394472,5.03101799301621,6.88580032960711));
#130250=CARTESIAN_POINT('Ctrl Pts',(19.7118759634393,5.03451137520289,6.7977825101827));
#130251=CARTESIAN_POINT('Ctrl Pts',(19.7049446719573,5.04038053144858,6.64990566562309));
#130252=CARTESIAN_POINT('Ctrl Pts',(19.6980133804754,5.05269303632925,6.50225813648039));
#130253=CARTESIAN_POINT('Ctrl Pts',(19.6910820889935,5.07140714354957,6.35540892379343));
#130254=CARTESIAN_POINT('Ctrl Pts',(19.684152155773,5.09011758353832,6.20858848779688));
#130255=CARTESIAN_POINT('Ctrl Pts',(19.6772222225525,5.11522708127017,6.06256638434082));
#130256=CARTESIAN_POINT('Ctrl Pts',(19.6702922893321,5.14664214325448,5.91790546648205));
#130257=CARTESIAN_POINT('Ctrl Pts',(19.6633621517524,5.1780581316483,5.77324028266798));
#130258=CARTESIAN_POINT('Ctrl Pts',(19.6564320141728,5.21577998959382,5.62993668900666));
#130259=CARTESIAN_POINT('Ctrl Pts',(19.6495018765932,5.25966320185875,5.48854687156054));
#130260=CARTESIAN_POINT('Ctrl Pts',(19.6425721311451,5.30354393105684,5.34716505444874));
#130261=CARTESIAN_POINT('Ctrl Pts',(19.6356423856971,5.35358521806554,5.20769711279096));
#130262=CARTESIAN_POINT('Ctrl Pts',(19.6287126402491,5.40959281113345,5.07067962005118));
#130263=CARTESIAN_POINT('Ctrl Pts',(19.6217813588474,5.46561281808696,4.93363175786706));
#130264=CARTESIAN_POINT('Ctrl Pts',(19.6148500774458,5.52760164817835,4.79903573639757));
#130265=CARTESIAN_POINT('Ctrl Pts',(19.6079187960441,5.59531683860089,4.6674082957181));
#130266=CARTESIAN_POINT('Ctrl Pts',(19.6037893035398,5.63565993752792,4.58898779911004));
#130267=CARTESIAN_POINT('Ctrl Pts',(19.5996598110354,5.67803469414855,4.51162059036806));
#130268=CARTESIAN_POINT('Ctrl Pts',(19.5955303185311,5.72238203724709,4.43541187275996));
#130269=CARTESIAN_POINT('Ctrl Pts',(19.5885944856084,5.79686716150288,4.30741286754781));
#130270=CARTESIAN_POINT('Ctrl Pts',(19.5816586526857,5.87694484651429,4.18263962042732));
#130271=CARTESIAN_POINT('Ctrl Pts',(19.5747228197629,5.96231102063768,4.06157576067015));
#130272=CARTESIAN_POINT('Ctrl Pts',(19.5677882683408,6.04766142206249,3.94053426930173));
#130273=CARTESIAN_POINT('Ctrl Pts',(19.5608537169187,6.138298172888,3.82320106750737));
#130274=CARTESIAN_POINT('Ctrl Pts',(19.5539191654965,6.23387438004653,3.71003008689105));
#130275=CARTESIAN_POINT('Ctrl Pts',(19.5469843393753,6.32945437327471,3.59685462322159));
#130276=CARTESIAN_POINT('Ctrl Pts',(19.5400495132541,6.42997400380587,3.48784196492398));
#130277=CARTESIAN_POINT('Ctrl Pts',(19.5331146871329,6.53504630945991,3.38341270441833));
#130278=CARTESIAN_POINT('Ctrl Pts',(19.526180224502,6.64011310772749,3.2789889175938));
#130279=CARTESIAN_POINT('Ctrl Pts',(19.5192457618712,6.74973186874695,3.17914827984244));
#130280=CARTESIAN_POINT('Ctrl Pts',(19.5123112992403,6.86347901257573,3.08427428058295));
#130281=CARTESIAN_POINT('Ctrl Pts',(19.5053752975239,6.97725140228127,2.98937922429105));
#130282=CARTESIAN_POINT('Ctrl Pts',(19.4984392958074,7.09515375203486,2.89945322061358));
#130283=CARTESIAN_POINT('Ctrl Pts',(19.491503294091,7.21672918432727,2.81483964759232));
#130284=CARTESIAN_POINT('Ctrl Pts',(19.4873970872683,7.28870348450164,2.76474726800027));
#130285=CARTESIAN_POINT('Ctrl Pts',(19.4832908804456,7.36196451810915,2.71651600682106));
#130286=CARTESIAN_POINT('Ctrl Pts',(19.4791846736229,7.43641261061583,2.67021001512314));
#130287=CARTESIAN_POINT('Ctrl Pts',(19.4722525172567,7.56209693210968,2.59203558577654));
#130288=CARTESIAN_POINT('Ctrl Pts',(19.4653203608905,7.69120946211311,2.51932363092219));
#130289=CARTESIAN_POINT('Ctrl Pts',(19.4583882045243,7.82325572183359,2.45235903688245));
#130290=CARTESIAN_POINT('Ctrl Pts',(19.4514573849167,7.95527651848407,2.38540735592446));
#130291=CARTESIAN_POINT('Ctrl Pts',(19.4445265653092,8.09022962124302,2.32420097417425));
#130292=CARTESIAN_POINT('Ctrl Pts',(19.4375957457017,8.22759659625989,2.26897849900872));
#130293=CARTESIAN_POINT('Ctrl Pts',(19.4306646979627,8.36496809277999,2.21375420616759));
#130294=CARTESIAN_POINT('Ctrl Pts',(19.4237336502237,8.50475331485511,2.1645143406319));
#130295=CARTESIAN_POINT('Ctrl Pts',(19.4168026024848,8.64641401791103,2.12144929618117));
#130296=CARTESIAN_POINT('Ctrl Pts',(19.4098719355473,8.78806693792938,2.07838661778434));
#130297=CARTESIAN_POINT('Ctrl Pts',(19.4029412686098,8.93159481592078,2.0414981770105));
#130298=CARTESIAN_POINT('Ctrl Pts',(19.3960106016723,9.07644441148998,2.01092444159163));
#130299=CARTESIAN_POINT('Ctrl Pts',(19.3890783892253,9.22132630791024,1.98034388835824));
#130300=CARTESIAN_POINT('Ctrl Pts',(19.3821461767782,9.36753018698955,1.95608092251632));
#130301=CARTESIAN_POINT('Ctrl Pts',(19.3752139643311,9.51449215978495,1.93822497966632));
#130302=CARTESIAN_POINT('Ctrl Pts',(19.3710889857923,9.60194115077144,1.92759988968118));
#130303=CARTESIAN_POINT('Ctrl Pts',(19.3669640072535,9.68965839362783,1.91924240856535));
#130304=CARTESIAN_POINT('Ctrl Pts',(19.3628390287147,9.77752407795016,1.91316267703624));
#130305=CARTESIAN_POINT('Ctrl Pts',(19.3559048075467,9.9252291102158,1.90294245342334));
#130306=CARTESIAN_POINT('Ctrl Pts',(19.3489705863787,10.0734048576221,1.89915811700655));
#130307=CARTESIAN_POINT('Ctrl Pts',(19.3420363652107,10.2214806592299,1.9018296852373));
#130308=CARTESIAN_POINT('Ctrl Pts',(19.335103451794,10.3695285346548,1.90450074962676));
#130309=CARTESIAN_POINT('Ctrl Pts',(19.3281705383774,10.5174761716726,1.91362528350658));
#130310=CARTESIAN_POINT('Ctrl Pts',(19.3212376249607,10.6647534305791,1.92917119545007));
#130311=CARTESIAN_POINT('Ctrl Pts',(19.3143044602487,10.8120360278019,1.94471767088173));
#130312=CARTESIAN_POINT('Ctrl Pts',(19.3073712955368,10.9586478693285,1.96668595872507));
#130313=CARTESIAN_POINT('Ctrl Pts',(19.3004381308248,11.1040238996176,1.99499209100783));
#130314=CARTESIAN_POINT('Ctrl Pts',(19.2935053388582,11.2493921141048,2.02329670147767));
#130315=CARTESIAN_POINT('Ctrl Pts',(19.2865725468916,11.3935243261183,2.05793841047807));
#130316=CARTESIAN_POINT('Ctrl Pts',(19.279639754925,11.535865618028,2.09878211579726));
#130317=CARTESIAN_POINT('Ctrl Pts',(19.2727054235545,11.678238516357,2.13963489032792));
#130318=CARTESIAN_POINT('Ctrl Pts',(19.2657710921841,11.8188193822447,2.18669232169525));
#130319=CARTESIAN_POINT('Ctrl Pts',(19.2588367608137,11.9570677921862,2.23976923196325));
#130320=CARTESIAN_POINT('Ctrl Pts',(19.2547223018113,12.0390969575754,2.27126221370942));
#130321=CARTESIAN_POINT('Ctrl Pts',(19.2506078428089,12.1203052653314,2.30487346637448));
#130322=CARTESIAN_POINT('Ctrl Pts',(19.2464933838065,12.2005829824517,2.34055622635073));
#130323=CARTESIAN_POINT('Ctrl Pts',(19.2395600659607,12.3358598021767,2.40068561793972));
#130324=CARTESIAN_POINT('Ctrl Pts',(19.2326267481149,12.4685396684855,2.4667205822027));
#130325=CARTESIAN_POINT('Ctrl Pts',(19.225693430269,12.5981090877672,2.53841169853235));
#130326=CARTESIAN_POINT('Ctrl Pts',(19.2187614321196,12.7276538446444,2.6100891690857));
#130327=CARTESIAN_POINT('Ctrl Pts',(19.2118294339701,12.8540890465733,2.68742048375259));
#130328=CARTESIAN_POINT('Ctrl Pts',(19.2048974358206,12.9769260564387,2.77011042069487));
#130329=CARTESIAN_POINT('Ctrl Pts',(19.1979651953757,13.0997673598497,2.85280324791448));
#130330=CARTESIAN_POINT('Ctrl Pts',(19.1910329549307,13.2190099433899,2.9408548903621));
#130331=CARTESIAN_POINT('Ctrl Pts',(19.1841007144858,13.3341939513471,3.03392666757164));
#130332=CARTESIAN_POINT('Ctrl Pts',(19.1771688496638,13.4493717180665,3.12699340169313));
#130333=CARTESIAN_POINT('Ctrl Pts',(19.1702369848419,13.5604910926603,3.22507951774791));
#130334=CARTESIAN_POINT('Ctrl Pts',(19.1633051200199,13.667125119773,3.3278058994722));
#130335=CARTESIAN_POINT('Ctrl Pts',(19.1563717121302,13.7737828841536,3.430555148603));
#130336=CARTESIAN_POINT('Ctrl Pts',(19.1494383042404,13.8759530677986,3.53794649789823));
#130337=CARTESIAN_POINT('Ctrl Pts',(19.1425048963507,13.9732449701325,3.64956337105432));
#130338=CARTESIAN_POINT('Ctrl Pts',(19.1383858438666,14.0310448945516,3.71587358472634));
#130339=CARTESIAN_POINT('Ctrl Pts',(19.1342667913824,14.0871237909435,3.78367446321953));
#130340=CARTESIAN_POINT('Ctrl Pts',(19.1301477388983,14.1414063406675,3.85287297464629));
#130341=CARTESIAN_POINT('Ctrl Pts',(19.1232141285398,14.2327802793352,3.96935498536888));
#130342=CARTESIAN_POINT('Ctrl Pts',(19.1162805181812,14.3190936323279,4.08983919704816));
#130343=CARTESIAN_POINT('Ctrl Pts',(19.1093469078227,14.400009475508,4.213864716207));
#130344=CARTESIAN_POINT('Ctrl Pts',(19.1024146136957,14.4809099581506,4.3378666911678));
#130345=CARTESIAN_POINT('Ctrl Pts',(19.0954823195687,14.5564147947404,4.46540835564231));
#130346=CARTESIAN_POINT('Ctrl Pts',(19.0885500254416,14.6262304728754,4.59599998870346));
#130347=CARTESIAN_POINT('Ctrl Pts',(19.0816174867073,14.6960486144694,4.72659622971433));
#130348=CARTESIAN_POINT('Ctrl Pts',(19.0746849479731,14.7601770371195,4.86024236471895));
#130349=CARTESIAN_POINT('Ctrl Pts',(19.0677524092388,14.8183680106684,4.99642375275354));
#130350=CARTESIAN_POINT('Ctrl Pts',(19.0608202455346,14.8765558362549,5.13259777377116));
#130351=CARTESIAN_POINT('Ctrl Pts',(19.0538880818305,14.928806726421,5.2713064690269));
#130352=CARTESIAN_POINT('Ctrl Pts',(19.0469559181264,14.9749209568293,5.41201487692134));
#130353=CARTESIAN_POINT('Ctrl Pts',(19.0400222130546,15.0210454407442,5.55275457135289));
#130354=CARTESIAN_POINT('Ctrl Pts',(19.0330885079828,15.061030435488,5.69549455262194));
#130355=CARTESIAN_POINT('Ctrl Pts',(19.0261548029109,15.0947257927471,5.83968373835435));
#130356=CARTESIAN_POINT('Ctrl Pts',(19.0220372332707,15.1147357266325,5.92531025512671));
#130357=CARTESIAN_POINT('Ctrl Pts',(19.0179196636304,15.1325285371395,6.01144756489171));
#130358=CARTESIAN_POINT('Ctrl Pts',(19.0138020939901,15.1480812641024,6.09797832864145));
#130359=CARTESIAN_POINT('Ctrl Pts',(19.0068685366312,15.1742704324482,6.243687100122));
#130360=CARTESIAN_POINT('Ctrl Pts',(18.9999349792723,15.1941141114036,6.39056233036988));
#130361=CARTESIAN_POINT('Ctrl Pts',(18.9930014219134,15.2075304301788,6.53803901660621));
#130362=CARTESIAN_POINT('Ctrl Pts',(18.9860691810523,15.2209442015525,6.68548770094879));
#130363=CARTESIAN_POINT('Ctrl Pts',(18.9791369401912,15.2279330176624,6.83353728439083));
#130364=CARTESIAN_POINT('Ctrl Pts',(18.9722046993301,15.2284668647841,6.98161762166019));
#130365=CARTESIAN_POINT('Ctrl Pts',(18.9652722137388,15.2290007307523,7.12970318663661));
#130366=CARTESIAN_POINT('Ctrl Pts',(18.9583397281476,15.2230791672004,7.277819177055));
#130367=CARTESIAN_POINT('Ctrl Pts',(18.9514072425563,15.2107242822434,7.42539486778772));
#130368=CARTESIAN_POINT('Ctrl Pts',(18.944475131797,15.1983700653015,7.57296257926426));
#130369=CARTESIAN_POINT('Ctrl Pts',(18.9375430210376,15.1795832514988,7.71998972015295));
#130370=CARTESIAN_POINT('Ctrl Pts',(18.9306109102783,15.1544378816705,7.8659100908022));
#130371=CARTESIAN_POINT('Ctrl Pts',(18.9236772573793,15.1292869179224,8.01186292336617));
#130372=CARTESIAN_POINT('Ctrl Pts',(18.9167436044803,15.0977746278607,8.15670816782282));
#130373=CARTESIAN_POINT('Ctrl Pts',(18.9098099515813,15.0600264057109,8.29988859622179));
#130374=CARTESIAN_POINT('Ctrl Pts',(18.9056921174149,15.0376080756969,8.38492216635021));
#130375=CARTESIAN_POINT('Ctrl Pts',(18.9015742832484,15.0129912650688,8.46936874673091));
#130376=CARTESIAN_POINT('Ctrl Pts',(18.8974564490819,14.9862106421525,8.55311388455654));
#130377=CARTESIAN_POINT('Ctrl Pts',(18.890522946704,14.9411181238125,8.69412177578796));
#130378=CARTESIAN_POINT('Ctrl Pts',(18.883589444326,14.8898727356053,8.83318887004119));
#130379=CARTESIAN_POINT('Ctrl Pts',(18.8766559419481,14.8326667134249,8.96977761834485));
#130380=CARTESIAN_POINT('Ctrl Pts',(18.8697236785937,14.7754709140157,9.10634195810776));
#130381=CARTESIAN_POINT('Ctrl Pts',(18.8627914152393,14.712316733052,9.2404285306325));
#130382=CARTESIAN_POINT('Ctrl Pts',(18.8558591518849,14.6434446407832,9.37151950865782));
#130383=CARTESIAN_POINT('Ctrl Pts',(18.8547452676674,14.6323781921101,9.39258336096776));
#130384=CARTESIAN_POINT('Ctrl Pts',(18.85363138345,14.6211642148427,9.41356991806466));
#130385=CARTESIAN_POINT('Ctrl Pts',(18.8525174992326,14.6098038194187,9.43447708670712));
#130386=CARTESIAN_POINT('Ctrl Pts',(20.352563293369,14.6098038194187,9.43447708670712));
#130387=CARTESIAN_POINT('Ctrl Pts',(20.3452868626689,14.5356719094128,9.57090617094612));
#130388=CARTESIAN_POINT('Ctrl Pts',(20.3380104319687,14.4553225791197,9.70391405302278));
#130389=CARTESIAN_POINT('Ctrl Pts',(20.3307340012685,14.3690871677716,9.83296693359918));
#130390=CARTESIAN_POINT('Ctrl Pts',(20.3234553596846,14.2828255545013,9.96205902583457));
#130391=CARTESIAN_POINT('Ctrl Pts',(20.3161767181007,14.1906744289206,10.0871935054699));
#130392=CARTESIAN_POINT('Ctrl Pts',(20.3088980765167,14.0930082832942,10.207865815189));
#130393=CARTESIAN_POINT('Ctrl Pts',(20.3038001136712,14.0246028843024,10.2923847387183));
#130394=CARTESIAN_POINT('Ctrl Pts',(20.2987021508257,13.9534929304548,10.3747153144459));
#130395=CARTESIAN_POINT('Ctrl Pts',(20.2936041879802,13.8798190021703,10.4546936741136));
#130396=CARTESIAN_POINT('Ctrl Pts',(20.2868777084082,13.7826103349796,10.5602206892792));
#130397=CARTESIAN_POINT('Ctrl Pts',(20.2801512288361,13.6808807511221,10.6617110339456));
#130398=CARTESIAN_POINT('Ctrl Pts',(20.2734247492641,13.5749966495666,10.7587702560579));
#130399=CARTESIAN_POINT('Ctrl Pts',(20.2667018516651,13.469168933226,10.8557777923645));
#130400=CARTESIAN_POINT('Ctrl Pts',(20.2599789540661,13.3591913769016,10.9483586585881));
#130401=CARTESIAN_POINT('Ctrl Pts',(20.2532560564671,13.2454670553348,11.0361553872551));
#130402=CARTESIAN_POINT('Ctrl Pts',(20.2465348108106,13.1317706779763,11.1239305426118));
#130403=CARTESIAN_POINT('Ctrl Pts',(20.2398135651542,13.0143296577915,11.2069236743742));
#130404=CARTESIAN_POINT('Ctrl Pts',(20.2330923194978,12.8935800092736,11.2848176976779));
#130405=CARTESIAN_POINT('Ctrl Pts',(20.2263722417576,12.7728513428002,11.3626981857385));
#130406=CARTESIAN_POINT('Ctrl Pts',(20.2196521640174,12.6488155039474,11.4354811335249));
#130407=CARTESIAN_POINT('Ctrl Pts',(20.2129320862772,12.5219371004028,11.5028930389935));
#130408=CARTESIAN_POINT('Ctrl Pts',(20.2062101801347,12.3950241757136,11.5703232859298));
#130409=CARTESIAN_POINT('Ctrl Pts',(20.1994882739921,12.2652674652434,11.6323793963712));
#130410=CARTESIAN_POINT('Ctrl Pts',(20.1927663678496,12.1331560519276,11.6888339089345));
#130411=CARTESIAN_POINT('Ctrl Pts',(20.1875970929237,12.0315598377311,11.7322485133716));
#130412=CARTESIAN_POINT('Ctrl Pts',(20.1824278179979,11.9285716059888,11.7723513056034));
#130413=CARTESIAN_POINT('Ctrl Pts',(20.1772585430721,11.8244215995656,11.8090583040057));
#130414=CARTESIAN_POINT('Ctrl Pts',(20.1702029153173,11.6822655551441,11.8591602855097));
#130415=CARTESIAN_POINT('Ctrl Pts',(20.1631472875625,11.5378982969924,11.9029508158294));
#130416=CARTESIAN_POINT('Ctrl Pts',(20.1560916598077,11.3918866567047,11.9402612207224));
#130417=CARTESIAN_POINT('Ctrl Pts',(20.1490358127607,11.245870478308,11.9775727852401));
#130418=CARTESIAN_POINT('Ctrl Pts',(20.1419799657137,11.0982101122984,12.0084037507865));
#130419=CARTESIAN_POINT('Ctrl Pts',(20.1349241186668,10.9494848386558,12.0326360750977));
#130420=CARTESIAN_POINT('Ctrl Pts',(20.1278666858757,10.8007261402202,12.0568738454262));
#130421=CARTESIAN_POINT('Ctrl Pts',(20.1208092530846,10.6509023569821,12.0745099618943));
#130422=CARTESIAN_POINT('Ctrl Pts',(20.1137518202935,10.5006010709216,12.0854778531777));
#130423=CARTESIAN_POINT('Ctrl Pts',(20.1079500454062,10.3770413782099,12.0944943380808));
#130424=CARTESIAN_POINT('Ctrl Pts',(20.1021482705188,10.2531592030081,12.0990052716912));
#130425=CARTESIAN_POINT('Ctrl Pts',(20.0963464956315,10.1292828162553,12.0989999953747));
#130426=CARTESIAN_POINT('',(20.2216535043684,10.1337426824875,12.0989982349129));
#130427=CARTESIAN_POINT('Ctrl Pts',(20.4776000250576,14.6098038194187,9.43447708670711));
#130428=CARTESIAN_POINT('Ctrl Pts',(20.4711196680077,14.5438130309703,9.55592361136169));
#130429=CARTESIAN_POINT('Ctrl Pts',(20.4646393109577,14.4727878484368,9.67485523573746));
#130430=CARTESIAN_POINT('Ctrl Pts',(20.4581589539078,14.3969502782224,9.79081871910371));
#130431=CARTESIAN_POINT('Ctrl Pts',(20.4516843951578,14.3211805636795,9.9066784441347));
#130432=CARTESIAN_POINT('Ctrl Pts',(20.4452098364078,14.2406072440856,10.0195749767462));
#130433=CARTESIAN_POINT('Ctrl Pts',(20.4387352776578,14.1554982256597,10.1290796229858));
#130434=CARTESIAN_POINT('Ctrl Pts',(20.4319680553625,14.0665421022753,10.2435341073896));
#130435=CARTESIAN_POINT('Ctrl Pts',(20.4252008330672,13.9726308486994,10.3542824951181));
#130436=CARTESIAN_POINT('Ctrl Pts',(20.4184336107719,13.8741212483996,10.4608687790834));
#130437=CARTESIAN_POINT('Ctrl Pts',(20.4119648781616,13.7799567247469,10.5627537387925));
#130438=CARTESIAN_POINT('Ctrl Pts',(20.4054961455513,13.6815911429066,10.6608355944725));
#130439=CARTESIAN_POINT('Ctrl Pts',(20.3990274129409,13.5793769002379,10.7547503742865));
#130440=CARTESIAN_POINT('Ctrl Pts',(20.3925591385534,13.4771698980755,10.8486585014998));
#130441=CARTESIAN_POINT('Ctrl Pts',(20.3860908641659,13.3711150722958,10.938399867969));
#130442=CARTESIAN_POINT('Ctrl Pts',(20.3796225897784,13.2616004380997,11.0236485738265));
#130443=CARTESIAN_POINT('Ctrl Pts',(20.3731532953867,13.1520685341682,11.1089107228425));
#130444=CARTESIAN_POINT('Ctrl Pts',(20.366684000995,13.0390760535248,11.1896785559707));
#130445=CARTESIAN_POINT('Ctrl Pts',(20.3602147066033,12.9230422847047,11.2656678848179));
#130446=CARTESIAN_POINT('Ctrl Pts',(20.3537429132159,12.8069636937012,11.3416865672548));
#130447=CARTESIAN_POINT('Ctrl Pts',(20.3472711198284,12.6878418136861,11.412922855206));
#130448=CARTESIAN_POINT('Ctrl Pts',(20.3407993264409,12.5661224834895,11.4791374027767));
#130449=CARTESIAN_POINT('Ctrl Pts',(20.3343198330908,12.4442583349656,11.5454307306038));
#130450=CARTESIAN_POINT('Ctrl Pts',(20.3278403397406,12.3197909209688,11.6066902022129));
#130451=CARTESIAN_POINT('Ctrl Pts',(20.3213608463905,12.1931884004942,11.6627235802335));
#130452=CARTESIAN_POINT('Ctrl Pts',(20.3148768275244,12.0664974561729,11.7187960940218));
#130453=CARTESIAN_POINT('Ctrl Pts',(20.3083928086584,11.9376688092067,11.7696351036927));
#130454=CARTESIAN_POINT('Ctrl Pts',(20.3019087897923,11.8071866552316,11.8150979727164));
#130455=CARTESIAN_POINT('Ctrl Pts',(20.2954150217898,11.676508313007,11.8606291980664));
#130456=CARTESIAN_POINT('Ctrl Pts',(20.2889212537874,11.5441718846024,11.9007680384156));
#130457=CARTESIAN_POINT('Ctrl Pts',(20.282427485785,11.4106729541157,11.9354226629178));
#130458=CARTESIAN_POINT('Ctrl Pts',(20.2803923047135,11.3688336866381,11.9462836046392));
#130459=CARTESIAN_POINT('Ctrl Pts',(20.278357123642,11.3268802787869,11.956606253736));
#130460=CARTESIAN_POINT('Ctrl Pts',(20.2763219425705,11.2848280760658,11.9663888326081));
#130461=CARTESIAN_POINT('Ctrl Pts',(20.2664266823321,11.0803659299939,12.0139527398677));
#130462=CARTESIAN_POINT('Ctrl Pts',(20.2565314220938,10.8730095382161,12.0488763230015));
#130463=CARTESIAN_POINT('Ctrl Pts',(20.2466361618554,10.6640303707002,12.0709050753094));
#130464=CARTESIAN_POINT('Ctrl Pts',(20.2383086093597,10.4881598078176,12.0894438086868));
#130465=CARTESIAN_POINT('Ctrl Pts',(20.2299810568641,10.3111395726563,12.098850629708));
#130466=CARTESIAN_POINT('Ctrl Pts',(20.2216535043684,10.1337426824875,12.0989982349129));
#130467=CARTESIAN_POINT('Ctrl Pts',(20.2216531628861,10.1337360354165,12.0997534730252));
#130468=CARTESIAN_POINT('Ctrl Pts',(20.1623123261755,8.86943546207591,12.0878187862941));
#130469=CARTESIAN_POINT('Ctrl Pts',(20.0641896078287,6.76854703791684,11.2892745934799));
#130470=CARTESIAN_POINT('Ctrl Pts',(19.9272850078459,5.12804044036981,8.75245917967931));
#130471=CARTESIAN_POINT('Ctrl Pts',(19.8109393629377,4.88151594588123,6.21192105474875));
#130472=CARTESIAN_POINT('Ctrl Pts',(19.6945937180295,5.86543450296868,3.84345751957051));
#130473=CARTESIAN_POINT('Ctrl Pts',(19.5782480731213,7.83815969325507,2.21543015947418));
#130474=CARTESIAN_POINT('Ctrl Pts',(19.4619024282131,10.3463489318624,1.69885207129888));
#130475=CARTESIAN_POINT('Ctrl Pts',(19.3455567833049,12.803119455071,2.41785981379941));
#130476=CARTESIAN_POINT('Ctrl Pts',(19.2292111383967,14.6377971005625,4.2031950129451));
#130477=CARTESIAN_POINT('Ctrl Pts',(19.1128654934886,15.4225339830853,6.640033572117));
#130478=CARTESIAN_POINT('Ctrl Pts',(19.029068925348,15.1001465815671,8.45540708667062));
#130479=CARTESIAN_POINT('Ctrl Pts',(18.9840542388435,14.6736170860257,9.31766124714267));
#130480=CARTESIAN_POINT('Ctrl Pts',(18.9778214339751,14.6099559957068,9.43455988473872));
#130481=CARTESIAN_POINT('Origin',(-18.734,19.211,-1.76670989022852));
#130482=CARTESIAN_POINT('',(-17.1724222331904,17.1782439613541,0.749817809475409));
#130483=CARTESIAN_POINT('',(-17.1763093433855,17.1833020606949,0.683386614791102));
#130484=CARTESIAN_POINT('',(-17.174464231106,17.180864983421,-1.76670989022852));
#130485=CARTESIAN_POINT('',(-21.2939992552734,19.212952690406,0.233290109771496));
#130486=CARTESIAN_POINT('Ctrl Pts',(-21.2960081472498,19.2129542227284,
0.233290109771496));
#130487=CARTESIAN_POINT('Ctrl Pts',(-21.2971424692952,19.3442911272882,
0.239839092339242));
#130488=CARTESIAN_POINT('Ctrl Pts',(-21.2281784359338,20.3246261525587,
0.288780010467465));
#130489=CARTESIAN_POINT('Ctrl Pts',(-19.9618263685217,21.9781789381743,
0.380112864156167));
#130490=CARTESIAN_POINT('Ctrl Pts',(-17.0720918237967,21.7409376748804,
0.507288670837602));
#130491=CARTESIAN_POINT('Ctrl Pts',(-15.7493319130901,19.2624152772813,
0.630523652610683));
#130492=CARTESIAN_POINT('Ctrl Pts',(-16.5648620620492,17.6518059357956,
0.711366698823284));
#130493=CARTESIAN_POINT('Ctrl Pts',(-17.1724222331904,17.1782439613541,
0.749817809475409));
#130494=CARTESIAN_POINT('',(-18.0722320621911,16.7380133044256,1.80302994756687E-11));
#130495=CARTESIAN_POINT('Ctrl Pts',(-18.0722320621911,16.7380133044256,
1.80300219199125E-11));
#130496=CARTESIAN_POINT('Ctrl Pts',(-18.1529464922157,16.7164142307207,
0.00418158398862037));
#130497=CARTESIAN_POINT('Ctrl Pts',(-18.2348706569439,16.6987304519573,
0.00836316795921058));
#130498=CARTESIAN_POINT('Ctrl Pts',(-18.3175895998167,16.6850937510234,
0.012544751929801));
#130499=CARTESIAN_POINT('Ctrl Pts',(-18.400190747281,16.6714764693507,0.0167203811411207));
#130500=CARTESIAN_POINT('Ctrl Pts',(-18.4835839741038,16.6618948926126,
0.0208960103524402));
#130501=CARTESIAN_POINT('Ctrl Pts',(-18.5673406239762,16.656430632693,0.02507163956376));
#130502=CARTESIAN_POINT('Ctrl Pts',(-18.6514938546105,16.6509404999577,
0.0292670400316576));
#130503=CARTESIAN_POINT('Ctrl Pts',(-18.7360135046785,16.6496069028829,
0.0334624404995552));
#130504=CARTESIAN_POINT('Ctrl Pts',(-18.8204558534901,16.6524603021651,
0.0376578409674528));
#130505=CARTESIAN_POINT('Ctrl Pts',(-18.9043486080215,16.6552951300557,
0.0418259356091481));
#130506=CARTESIAN_POINT('Ctrl Pts',(-18.9881645984016,16.6622626001438,
0.0459940302508442));
#130507=CARTESIAN_POINT('Ctrl Pts',(-19.0714668099551,16.6733404183818,
0.0501621248925395));
#130508=CARTESIAN_POINT('Ctrl Pts',(-19.1547409379247,16.684414501967,0.0543288143490282));
#130509=CARTESIAN_POINT('Ctrl Pts',(-19.2375011746968,16.6995961209329,
0.0584955038055169));
#130510=CARTESIAN_POINT('Ctrl Pts',(-19.3193159599542,16.7188111574315,
0.0626621932620057));
#130511=CARTESIAN_POINT('Ctrl Pts',(-19.4011278018881,16.7380255026606,
0.0668287328199814));
#130512=CARTESIAN_POINT('Ctrl Pts',(-19.481993811599,16.7612728705988,0.0709952723779566));
#130513=CARTESIAN_POINT('Ctrl Pts',(-19.5614943032478,16.7884283956728,
0.0751618119359323));
#130514=CARTESIAN_POINT('Ctrl Pts',(-19.6419503629735,16.8159103206512,
0.0793784318407133));
#130515=CARTESIAN_POINT('Ctrl Pts',(-19.721007396075,16.8473948424126,0.0835950517454946));
#130516=CARTESIAN_POINT('Ctrl Pts',(-19.7982496311477,16.8827017539409,
0.0878116716502757));
#130517=CARTESIAN_POINT('Ctrl Pts',(-19.8746816906651,16.9176383396154,
0.0919840644250511));
#130518=CARTESIAN_POINT('Ctrl Pts',(-19.9493364580842,16.9563172372311,
0.0961564571998266));
#130519=CARTESIAN_POINT('Ctrl Pts',(-20.0218360729121,16.9985176273456,
0.100328849974602));
#130520=CARTESIAN_POINT('Ctrl Pts',(-20.0954884255321,17.0413890001219,
0.104567583444386));
#130521=CARTESIAN_POINT('Ctrl Pts',(-20.1669160788343,17.0878945550855,
0.10880631691417));
#130522=CARTESIAN_POINT('Ctrl Pts',(-20.2357552271545,17.1377582780307,
0.113045050383954));
#130523=CARTESIAN_POINT('Ctrl Pts',(-20.3045943754748,17.187622000976,0.117283783853738));
#130524=CARTESIAN_POINT('Ctrl Pts',(-20.370844676157,17.2408435335627,0.121522517323522));
#130525=CARTESIAN_POINT('Ctrl Pts',(-20.4341804449292,17.2971069897509,
0.125761250793306));
#130526=CARTESIAN_POINT('Ctrl Pts',(-20.4958618563844,17.3519008204458,
0.129889266735435));
#130527=CARTESIAN_POINT('Ctrl Pts',(-20.5550187589506,17.4097927026216,
0.134017282677563));
#130528=CARTESIAN_POINT('Ctrl Pts',(-20.611317450137,17.4705175406195,0.138145298619692));
#130529=CARTESIAN_POINT('Ctrl Pts',(-20.6675250696014,17.5311441469278,
0.142266636866263));
#130530=CARTESIAN_POINT('Ctrl Pts',(-20.7208833454928,17.5945942591679,
0.146387975112834));
#130531=CARTESIAN_POINT('Ctrl Pts',(-20.7710927993391,17.6605636333984,
0.150509313359405));
#130532=CARTESIAN_POINT('Ctrl Pts',(-20.8212566260777,17.7264730589238,
0.154626906400053));
#130533=CARTESIAN_POINT('Ctrl Pts',(-20.8682770216554,17.7948968304612,
0.158744499440701));
#130534=CARTESIAN_POINT('Ctrl Pts',(-20.9118931634006,17.8654958681547,
0.162862092481349));
#130535=CARTESIAN_POINT('Ctrl Pts',(-20.9554835923167,17.9360532859129,
0.166977258095768));
#130536=CARTESIAN_POINT('Ctrl Pts',(-20.9956735017905,18.0087830229833,
0.171092423710186));
#130537=CARTESIAN_POINT('Ctrl Pts',(-21.0322449058945,18.0833163774666,
0.175207589324605));
#130538=CARTESIAN_POINT('Ctrl Pts',(-21.0688064212004,18.1578295783544,
0.179321642210581));
#130539=CARTESIAN_POINT('Ctrl Pts',(-21.1017511664475,18.2341450028519,
0.183435695096556));
#130540=CARTESIAN_POINT('Ctrl Pts',(-21.1309074513388,18.3118700484822,
0.187549747982531));
#130541=CARTESIAN_POINT('Ctrl Pts',(-21.1600799709319,18.3896383727037,
0.19166609164121));
#130542=CARTESIAN_POINT('Ctrl Pts',(-21.1854596457913,18.4688174432781,
0.195782435299889));
#130543=CARTESIAN_POINT('Ctrl Pts',(-21.2069235819087,18.5489962552674,
0.199898778958568));
#130544=CARTESIAN_POINT('Ctrl Pts',(-21.228393434594,18.6291971686732,0.204016257293894));
#130545=CARTESIAN_POINT('Ctrl Pts',(-21.2459452949941,18.710397909727,0.208133735629219));
#130546=CARTESIAN_POINT('Ctrl Pts',(-21.259507205158,18.7921762223861,0.212251213964544));
#130547=CARTESIAN_POINT('Ctrl Pts',(-21.2730871889122,18.8740635187863,
0.216374179551669));
#130548=CARTESIAN_POINT('Ctrl Pts',(-21.2826665466436,18.9565294532014,
0.220497145138794));
#130549=CARTESIAN_POINT('Ctrl Pts',(-21.2882251802136,19.0391461994527,
0.224620110725918));
#130550=CARTESIAN_POINT('Ctrl Pts',(-21.2921215137894,19.0970565470744,
0.227510110407777));
#130551=CARTESIAN_POINT('Ctrl Pts',(-21.2940434286409,19.1550409048321,
0.230400110089637));
#130552=CARTESIAN_POINT('Ctrl Pts',(-21.2939992552734,19.212952690406,0.233290109771496));
#130553=CARTESIAN_POINT('',(-19.3957372685685,16.7380050975816,0.));
#130554=CARTESIAN_POINT('Origin',(-18.734,19.211,0.));
#130555=CARTESIAN_POINT('',(-21.2914665409842,19.2078565222202,0.166709890228504));
#130556=CARTESIAN_POINT('Ctrl Pts',(-19.3957372685684,16.7380050975816,
-1.38777878078145E-15));
#130557=CARTESIAN_POINT('Ctrl Pts',(-20.2191097516036,16.9583275322964,
0.0423919355604767));
#130558=CARTESIAN_POINT('Ctrl Pts',(-21.1334433095435,17.8262083452195,
0.0979618989699786));
#130559=CARTESIAN_POINT('Ctrl Pts',(-21.2935044203301,18.9424073589822,
0.153531862379481));
#130560=CARTESIAN_POINT('Ctrl Pts',(-21.2914665409842,19.2078565222202,
0.166709890228504));
#130561=CARTESIAN_POINT('Ctrl Pts',(-21.2914665409842,19.2078565222202,
0.166709890228504));
#130562=CARTESIAN_POINT('Ctrl Pts',(-21.286948837742,19.7963214614176,0.195923797939959));
#130563=CARTESIAN_POINT('Ctrl Pts',(-20.7940989485341,21.2477394666147,
0.267529641211891));
#130564=CARTESIAN_POINT('Ctrl Pts',(-18.3819425041677,22.2167212403437,
0.381527420044301));
#130565=CARTESIAN_POINT('Ctrl Pts',(-16.0159517247016,20.543342471876,0.508703226725737));
#130566=CARTESIAN_POINT('Ctrl Pts',(-16.1161223324435,18.2509927299605,
0.609322958308004));
#130567=CARTESIAN_POINT('Ctrl Pts',(-16.9218454618781,17.3761757922868,
0.667550754329794));
#130568=CARTESIAN_POINT('Ctrl Pts',(-17.1763093433856,17.1833020606948,
0.683386614791108));
#130569=CARTESIAN_POINT('Origin',(-18.734,19.211,-1.76670989022852));
#130570=CARTESIAN_POINT('',(-17.1739275293696,17.1801545964507,1.55000082814523));
#130571=CARTESIAN_POINT('',(-17.174464231106,17.180864983421,1.4832495057092));
#130572=CARTESIAN_POINT('',(-17.174464231106,17.180864983421,-1.76670989022852));
#130573=CARTESIAN_POINT('',(-21.2964371839251,19.2091455679848,1.0332901097715));
#130574=CARTESIAN_POINT('Ctrl Pts',(-21.2964371839251,19.2091455679848,
1.0332901097715));
#130575=CARTESIAN_POINT('Ctrl Pts',(-21.2904549152958,19.943534301501,1.06991597459592));
#130576=CARTESIAN_POINT('Ctrl Pts',(-20.5735369997583,21.5381319822354,
1.14893377498083));
#130577=CARTESIAN_POINT('Ctrl Pts',(-17.8654473773764,22.1108088143134,
1.27034351092621));
#130578=CARTESIAN_POINT('Ctrl Pts',(-15.8255860744598,20.0502991614889,
1.39751931760764));
#130579=CARTESIAN_POINT('Ctrl Pts',(-16.2862201749042,17.975545059775,1.49073842334732));
#130580=CARTESIAN_POINT('Ctrl Pts',(-17.0385457352419,17.2819918267254,
1.54156559352652));
#130581=CARTESIAN_POINT('Ctrl Pts',(-17.1739275293697,17.1801545964506,
1.55000082814524));
#130582=CARTESIAN_POINT('Ctrl Pts',(-17.1724222331904,17.1782439613541,
0.749817809475409));
#130583=CARTESIAN_POINT('Ctrl Pts',(-17.2346906102321,17.1297089569582,
0.753758634383762));
#130584=CARTESIAN_POINT('Ctrl Pts',(-17.9939164716346,16.5951983123874,
0.800091394852595));
#130585=CARTESIAN_POINT('Ctrl Pts',(-20.0126665959802,16.4672456410459,
0.888816090881905));
#130586=CARTESIAN_POINT('Ctrl Pts',(-21.2376963893991,18.1288877895766,
0.979366032738913));
#130587=CARTESIAN_POINT('Ctrl Pts',(-21.2973789824122,19.0935295298239,
1.02752403903544));
#130588=CARTESIAN_POINT('Ctrl Pts',(-21.2964371839251,19.2091455679848,
1.0332901097715));
#130589=CARTESIAN_POINT('',(-21.293928833175,19.2123417088597,0.966709918231326));
#130590=CARTESIAN_POINT('Ctrl Pts',(-17.1763093433856,17.1833020606948,
0.683386614791108));
#130591=CARTESIAN_POINT('Ctrl Pts',(-17.6030346207299,16.8598608865745,
0.709942689890274));
#130592=CARTESIAN_POINT('Ctrl Pts',(-18.9689508657168,16.3489929032406,
0.77889070054992));
#130593=CARTESIAN_POINT('Ctrl Pts',(-20.8878309534133,17.3253417136014,
0.873331792362382));
#130594=CARTESIAN_POINT('Ctrl Pts',(-21.2880302326024,18.6981275094852,
0.941216809075682));
#130595=CARTESIAN_POINT('Ctrl Pts',(-21.2904840132329,19.212339338513,0.966709890228504));
#130596=CARTESIAN_POINT('Ctrl Pts',(-21.2939996483763,19.212341757587,0.96670991880698));
#130597=CARTESIAN_POINT('Ctrl Pts',(-21.2939507844152,19.3055715065957,
0.971325635711016));
#130598=CARTESIAN_POINT('Ctrl Pts',(-21.2888049367591,19.3986231740038,
0.975941352615052));
#130599=CARTESIAN_POINT('Ctrl Pts',(-21.2786449918221,19.4909676152607,
0.980557069519088));
#130600=CARTESIAN_POINT('Ctrl Pts',(-21.2684492414382,19.5836374946964,
0.985189053027621));
#130601=CARTESIAN_POINT('Ctrl Pts',(-21.2532041189474,19.6755948890935,
0.989821036536154));
#130602=CARTESIAN_POINT('Ctrl Pts',(-21.233043385604,19.7663216697276,0.994453020044687));
#130603=CARTESIAN_POINT('Ctrl Pts',(-21.2127838215892,19.8574932054453,
0.999107710169702));
#130604=CARTESIAN_POINT('Ctrl Pts',(-21.1875604649916,19.9474217736623,
1.00376240029472));
#130605=CARTESIAN_POINT('Ctrl Pts',(-21.1575575151709,20.035602310607,1.00841709041973));
#130606=CARTESIAN_POINT('Ctrl Pts',(-21.1382431318488,20.0923684853426,
1.01141354476365));
#130607=CARTESIAN_POINT('Ctrl Pts',(-21.1169489972049,20.1484106839985,
1.01440999910756));
#130608=CARTESIAN_POINT('Ctrl Pts',(-21.09373439265,20.2035994137337,1.01740645345148));
#130609=CARTESIAN_POINT('Ctrl Pts',(-21.0613129697488,20.2806757706407,
1.02159128947824));
#130610=CARTESIAN_POINT('Ctrl Pts',(-21.0250509503441,20.3563053098801,
1.02577612550499));
#130611=CARTESIAN_POINT('Ctrl Pts',(-20.9850989621192,20.4300789403257,
1.02996096153175));
#130612=CARTESIAN_POINT('Ctrl Pts',(-20.9452038243206,20.503747593209,1.0341398426681));
#130613=CARTESIAN_POINT('Ctrl Pts',(-20.9016293644686,20.57556518195,1.03831872380444));
#130614=CARTESIAN_POINT('Ctrl Pts',(-20.8545742375833,20.6451425671453,
1.04249760494079));
#130615=CARTESIAN_POINT('Ctrl Pts',(-20.8066785783708,20.7159627933522,
1.04675113224046));
#130616=CARTESIAN_POINT('Ctrl Pts',(-20.7551768665489,20.784461551568,1.05100465954013));
#130617=CARTESIAN_POINT('Ctrl Pts',(-20.7003275707681,20.8502546734529,
1.0552581868398));
#130618=CARTESIAN_POINT('Ctrl Pts',(-20.6465383521066,20.9147762059378,
1.05942950584669));
#130619=CARTESIAN_POINT('Ctrl Pts',(-20.5895301046939,20.9766953864738,
1.06360082485357));
#130620=CARTESIAN_POINT('Ctrl Pts',(-20.5295892191722,21.0356806175308,
1.06777214386046));
#130621=CARTESIAN_POINT('Ctrl Pts',(-20.4696684423106,21.0946460605258,
1.07194206349469));
#130622=CARTESIAN_POINT('Ctrl Pts',(-20.4068173088282,21.1506791864532,
1.07611198312893));
#130623=CARTESIAN_POINT('Ctrl Pts',(-20.341359759635,21.203484530205,1.08028190276316));
#130624=CARTESIAN_POINT('Ctrl Pts',(-20.2759045394191,21.2562879951444,
1.0844516740318));
#130625=CARTESIAN_POINT('Ctrl Pts',(-20.2078434464218,21.3058636181016,
1.08862144530044));
#130626=CARTESIAN_POINT('Ctrl Pts',(-20.137533188394,21.3519564659461,1.09279121656908));
#130627=CARTESIAN_POINT('Ctrl Pts',(-20.06475858035,21.3996648520281,1.09710713686606));
#130628=CARTESIAN_POINT('Ctrl Pts',(-19.9895746527788,21.4436414961582,
1.10142305716305));
#130629=CARTESIAN_POINT('Ctrl Pts',(-19.9124075159363,21.4836538949838,
1.10573897746003));
#130630=CARTESIAN_POINT('Ctrl Pts',(-19.8377462631117,21.5223669527317,
1.10991474488706));
#130631=CARTESIAN_POINT('Ctrl Pts',(-19.7612290811574,21.5573691376404,
1.11409051231409));
#130632=CARTESIAN_POINT('Ctrl Pts',(-19.6832632220047,21.5884985458143,
1.11826627974112));
#130633=CARTESIAN_POINT('Ctrl Pts',(-19.6013721661871,21.6211951662332,
1.12265227647308));
#130634=CARTESIAN_POINT('Ctrl Pts',(-19.5178832893452,21.6496186365429,
1.12703827320505));
#130635=CARTESIAN_POINT('Ctrl Pts',(-19.4332854194226,21.6736408390553,
1.13142426993701));
#130636=CARTESIAN_POINT('Ctrl Pts',(-19.3486875495,21.6976630415677,1.13581026666898));
#130637=CARTESIAN_POINT('Ctrl Pts',(-19.2629812685386,21.7172839209455,
1.14019626340094));
#130638=CARTESIAN_POINT('Ctrl Pts',(-19.1766642026735,21.7324377651791,
1.1445822601329));
#130639=CARTESIAN_POINT('Ctrl Pts',(-19.0943081662955,21.7468962101513,
1.14876698655741));
#130640=CARTESIAN_POINT('Ctrl Pts',(-19.0110898392259,21.7573423936353,
1.15295171298191));
#130641=CARTESIAN_POINT('Ctrl Pts',(-18.9274347142603,21.76368153347,1.15713643940641));
#130642=CARTESIAN_POINT('Ctrl Pts',(-18.8438986152898,21.7700116538642,
1.16131521172795));
#130643=CARTESIAN_POINT('Ctrl Pts',(-18.7599274076619,21.7722463033441,
1.1654939840495));
#130644=CARTESIAN_POINT('Ctrl Pts',(-18.6759558050627,21.7703418824835,
1.16967275637105));
#130645=CARTESIAN_POINT('Ctrl Pts',(-18.5904814673451,21.7684033805762,
1.17392631097285));
#130646=CARTESIAN_POINT('Ctrl Pts',(-18.5050071952172,21.7621761204825,
1.17817986557465));
#130647=CARTESIAN_POINT('Ctrl Pts',(-18.4199959426925,21.7516694889329,
1.18243342017646));
#130648=CARTESIAN_POINT('Ctrl Pts',(-18.336630364455,21.7413662480271,1.18660463314431));
#130649=CARTESIAN_POINT('Ctrl Pts',(-18.2537105165071,21.7269479013071,
1.19077584611216));
#130650=CARTESIAN_POINT('Ctrl Pts',(-18.1716702192111,21.7084757691793,
1.19494705908001));
#130651=CARTESIAN_POINT('Ctrl Pts',(-18.0896574199584,21.6900098284904,
1.19911687395207));
#130652=CARTESIAN_POINT('Ctrl Pts',(-18.00852403427,21.6674929018324,1.20328668882412));
#130653=CARTESIAN_POINT('Ctrl Pts',(-17.9286938256586,21.6410374411864,
1.20745650369618));
#130654=CARTESIAN_POINT('Ctrl Pts',(-17.8488664302294,21.6145829128194,
1.21162617162576));
#130655=CARTESIAN_POINT('Ctrl Pts',(-17.770342556957,21.584190271937,1.21579583955533));
#130656=CARTESIAN_POINT('Ctrl Pts',(-17.6935296236616,21.5500214612017,
1.21996550748491));
#130657=CARTESIAN_POINT('Ctrl Pts',(-17.6140201264992,21.5146531339729,
1.22428155409569));
#130658=CARTESIAN_POINT('Ctrl Pts',(-17.5363444143668,21.4752387864926,
1.22859760070648));
#130659=CARTESIAN_POINT('Ctrl Pts',(-17.4609286758951,21.4320108968084,
1.23291364731726));
#130660=CARTESIAN_POINT('Ctrl Pts',(-17.3879658074203,21.3901889788191,
1.23708931605134));
#130661=CARTESIAN_POINT('Ctrl Pts',(-17.3171185275023,21.3447980781215,
1.24126498478542));
#130662=CARTESIAN_POINT('Ctrl Pts',(-17.2487433858239,21.2960929931411,
1.2454406535195));
#130663=CARTESIAN_POINT('Ctrl Pts',(-17.1769202848533,21.2449318525502,
1.24982688906864));
#130664=CARTESIAN_POINT('Ctrl Pts',(-17.1078256590939,21.1901138543223,
1.25421312461778));
#130665=CARTESIAN_POINT('Ctrl Pts',(-17.041831884048,21.1319807566333,1.25859936016692));
#130666=CARTESIAN_POINT('Ctrl Pts',(-16.975838109002,21.0738476589442,1.26298559571606));
#130667=CARTESIAN_POINT('Ctrl Pts',(-16.9129455463668,21.0123999214843,
1.2673718312652));
#130668=CARTESIAN_POINT('Ctrl Pts',(-16.8534788428352,20.9480204884962,
1.27175806681434));
#130669=CARTESIAN_POINT('Ctrl Pts',(-16.7967467984314,20.8866016333375,
1.27594259521698));
#130670=CARTESIAN_POINT('Ctrl Pts',(-16.7429212490902,20.8222861496523,
1.28012712361962));
#130671=CARTESIAN_POINT('Ctrl Pts',(-16.6923122077179,20.755380444983,1.28431165202226));
#130672=CARTESIAN_POINT('Ctrl Pts',(-16.6417752234728,20.6885700006219,
1.2884902224955));
#130673=CARTESIAN_POINT('Ctrl Pts',(-16.5944459257278,20.6191770244767,
1.29266879296874));
#130674=CARTESIAN_POINT('Ctrl Pts',(-16.5505962863688,20.5475433862398,
1.29684736344198));
#130675=CARTESIAN_POINT('Ctrl Pts',(-16.5059592440483,20.4746234309496,
1.30110096802755));
#130676=CARTESIAN_POINT('Ctrl Pts',(-16.464928391305,20.3993819010164,1.30535457261313));
#130677=CARTESIAN_POINT('Ctrl Pts',(-16.4277464801528,20.3222131668551,
1.3096081771987));
#130678=CARTESIAN_POINT('Ctrl Pts',(-16.3912866103988,20.2465429845164,
1.3137791803658));
#130679=CARTESIAN_POINT('Ctrl Pts',(-16.3585277410935,20.1690202117747,
1.31795018353289));
#130680=CARTESIAN_POINT('Ctrl Pts',(-16.3296531424778,20.0900427684265,
1.32212118669999));
#130681=CARTESIAN_POINT('Ctrl Pts',(-16.3007882398716,20.0110918454832,
1.32629078925587));
#130682=CARTESIAN_POINT('Ctrl Pts',(-16.2758051753869,19.9306876537767,
1.33046039181175));
#130683=CARTESIAN_POINT('Ctrl Pts',(-16.2548387836586,19.8492473371575,
1.33462999436763));
#130684=CARTESIAN_POINT('Ctrl Pts',(-16.2338731420879,19.7678099343955,
1.3387994477391));
#130685=CARTESIAN_POINT('Ctrl Pts',(-16.2169240014122,19.6853369261729,
1.34296890111056));
#130686=CARTESIAN_POINT('Ctrl Pts',(-16.2040757356768,19.6022585037908,
1.34713835448203));
#130687=CARTESIAN_POINT('Ctrl Pts',(-16.1907749795004,19.5162542241176,
1.35145464773317));
#130688=CARTESIAN_POINT('Ctrl Pts',(-16.1818694215614,19.4296016124724,
1.35577094098432));
#130689=CARTESIAN_POINT('Ctrl Pts',(-16.1773942973163,19.3427849801954,
1.36008723423546));
#130690=CARTESIAN_POINT('Ctrl Pts',(-16.1730651983007,19.2588012119819,
1.36426268498077));
#130691=CARTESIAN_POINT('Ctrl Pts',(-16.1728818000995,19.1746644338099,
1.36843813572608));
#130692=CARTESIAN_POINT('Ctrl Pts',(-16.1768228602554,19.0908123302179,
1.37261358647138));
#130693=CARTESIAN_POINT('Ctrl Pts',(-16.1809633247949,19.0027175923177,
1.37700030097545));
#130694=CARTESIAN_POINT('Ctrl Pts',(-16.1896565650922,18.9149376772193,
1.38138701547952));
#130695=CARTESIAN_POINT('Ctrl Pts',(-16.2028167402278,18.8279708817217,
1.38577372998358));
#130696=CARTESIAN_POINT('Ctrl Pts',(-16.2159769153634,18.7410040862242,
1.39016044448765));
#130697=CARTESIAN_POINT('Ctrl Pts',(-16.2336038344097,18.6548509637838,
1.39454715899172));
#130698=CARTESIAN_POINT('Ctrl Pts',(-16.2555511520629,18.5699919593647,
1.39893387349578));
#130699=CARTESIAN_POINT('Ctrl Pts',(-16.2764836516381,18.4890567352055,
1.403117751496));
#130700=CARTESIAN_POINT('Ctrl Pts',(-16.3014237423075,18.4089973657718,
1.40730162949622));
#130701=CARTESIAN_POINT('Ctrl Pts',(-16.3302816105931,18.3302401550779,
1.41148550749644));
#130702=CARTESIAN_POINT('Ctrl Pts',(-16.3591010931301,18.2515877045299,
1.41566382024535));
#130703=CARTESIAN_POINT('Ctrl Pts',(-16.3918278499508,18.1742344017226,
1.41984213299427));
#130704=CARTESIAN_POINT('Ctrl Pts',(-16.4283216558807,18.0985938810581,
1.42402044574318));
#130705=CARTESIAN_POINT('Ctrl Pts',(-16.4647778709001,18.0230312748773,
1.42819445456772));
#130706=CARTESIAN_POINT('Ctrl Pts',(-16.5049932294979,17.9491783588005,
1.43236846339226));
#130707=CARTESIAN_POINT('Ctrl Pts',(-16.5487790116004,17.87742989241,1.4365424722168));
#130708=CARTESIAN_POINT('Ctrl Pts',(-16.592535947135,17.8057286947195,1.44071373115717));
#130709=CARTESIAN_POINT('Ctrl Pts',(-16.6398583963984,17.7361295853038,
1.44488499009755));
#130710=CARTESIAN_POINT('Ctrl Pts',(-16.6905117887282,17.6690026166063,
1.44905624903793));
#130711=CARTESIAN_POINT('Ctrl Pts',(-16.7411445842141,17.6019029432907,
1.4532258118477));
#130712=CARTESIAN_POINT('Ctrl Pts',(-16.7951053526934,17.5372737786853,
1.45739537465747));
#130713=CARTESIAN_POINT('Ctrl Pts',(-16.852117123077,17.4754548874938,1.46156493746724));
#130714=CARTESIAN_POINT('Ctrl Pts',(-16.9091415856326,17.4136222339513,
1.46573542852056));
#130715=CARTESIAN_POINT('Ctrl Pts',(-16.9692180992007,17.3546014460044,
1.46990591957388));
#130716=CARTESIAN_POINT('Ctrl Pts',(-17.0320310770586,17.2986972558349,
1.4740764106272));
#130717=CARTESIAN_POINT('Ctrl Pts',(-17.0780839607524,17.2577097202065,
1.47713410898787));
#130718=CARTESIAN_POINT('Ctrl Pts',(-17.1256069925995,17.2183967783007,
1.48019180734854));
#130719=CARTESIAN_POINT('Ctrl Pts',(-17.174464231106,17.180864983421,1.4832495057092));
#130720=CARTESIAN_POINT('Origin',(-18.734,19.211,-1.76670989022852));
#130721=CARTESIAN_POINT('',(-17.174464231106,17.180864983421,2.34989189146289));
#130722=CARTESIAN_POINT('',(-17.174464231106,17.180864983421,2.28327545488353));
#130723=CARTESIAN_POINT('',(-17.174464231106,17.180864983421,-1.76670989022852));
#130724=CARTESIAN_POINT('',(-21.2937660440385,19.2099923323681,1.83329006739986));
#130725=CARTESIAN_POINT('Ctrl Pts',(-21.293999801981,19.2099930953476,1.8332901097715));
#130726=CARTESIAN_POINT('Ctrl Pts',(-21.2940336318695,19.2960037294466,
1.83754657624536));
#130727=CARTESIAN_POINT('Ctrl Pts',(-21.289728450138,19.3819895209311,1.84180304271922));
#130728=CARTESIAN_POINT('Ctrl Pts',(-21.2811180404437,19.4674950058893,
1.84605950919308));
#130729=CARTESIAN_POINT('Ctrl Pts',(-21.2725026284394,19.5530501661775,
1.85031844850686));
#130730=CARTESIAN_POINT('Ctrl Pts',(-21.2595770559904,19.6381240344265,
1.85457738782065));
#130731=CARTESIAN_POINT('Ctrl Pts',(-21.2424267246312,19.7222683905308,
1.85883632713443));
#130732=CARTESIAN_POINT('Ctrl Pts',(-21.2252479654662,19.8065522214573,
1.86310232592114));
#130733=CARTESIAN_POINT('Ctrl Pts',(-21.203830549429,19.8899030384947,1.86736832470785));
#130734=CARTESIAN_POINT('Ctrl Pts',(-21.17831059956,19.9718848092049,1.87163432349455));
#130735=CARTESIAN_POINT('Ctrl Pts',(-21.1527682031271,20.0539386885619,
1.87590407452273));
#130736=CARTESIAN_POINT('Ctrl Pts',(-21.1231162332672,20.1346207166622,
1.88017382555091));
#130737=CARTESIAN_POINT('Ctrl Pts',(-21.0895392515833,20.2135142563825,
1.88444357657908));
#130738=CARTESIAN_POINT('Ctrl Pts',(-21.0558918629605,20.2925732264768,
1.88872228076758));
#130739=CARTESIAN_POINT('Ctrl Pts',(-21.0183032080418,20.3698358258174,
1.89300098495607));
#130740=CARTESIAN_POINT('Ctrl Pts',(-20.9770042478451,20.4449092122797,
1.89727968914457));
#130741=CARTESIAN_POINT('Ctrl Pts',(-20.9482314695913,20.4972124637696,
1.90026064087417));
#130742=CARTESIAN_POINT('Ctrl Pts',(-20.9176587209492,20.5484536579338,
1.90324159260377));
#130743=CARTESIAN_POINT('Ctrl Pts',(-20.8853760800086,20.5985089053289,
1.90622254433338));
#130744=CARTESIAN_POINT('Ctrl Pts',(-20.8400579767351,20.6687760459572,
1.91040717961721));
#130745=CARTESIAN_POINT('Ctrl Pts',(-20.79120937469,20.7369513806192,1.91459181490104));
#130746=CARTESIAN_POINT('Ctrl Pts',(-20.7390496454785,20.8026582293842,
1.91877645018487));
#130747=CARTESIAN_POINT('Ctrl Pts',(-20.6869641590402,20.8682715527659,
1.92295512916998));
#130748=CARTESIAN_POINT('Ctrl Pts',(-20.631577190453,20.9314230120947,1.92713380815509));
#130749=CARTESIAN_POINT('Ctrl Pts',(-20.5731519436452,20.9917639170272,
1.9313124871402));
#130750=CARTESIAN_POINT('Ctrl Pts',(-20.5136794822353,21.0531863728336,
1.93556606480165));
#130751=CARTESIAN_POINT('Ctrl Pts',(-20.4510590119848,21.1116961211984,
1.93981964246309));
#130752=CARTESIAN_POINT('Ctrl Pts',(-20.3856118363234,21.1669596984898,
1.94407322012453));
#130753=CARTESIAN_POINT('Ctrl Pts',(-20.3214334643362,21.2211518983045,
1.94824433502252));
#130754=CARTESIAN_POINT('Ctrl Pts',(-20.2545373774524,21.2722223583837,
1.9524154499205));
#130755=CARTESIAN_POINT('Ctrl Pts',(-20.185263188972,21.3198942970986,1.95658656481849));
#130756=CARTESIAN_POINT('Ctrl Pts',(-20.1160122460259,21.3675502390951,
1.96075628006393));
#130757=CARTESIAN_POINT('Ctrl Pts',(-20.0443851649613,21.4118096640091,
1.96492599530937));
#130758=CARTESIAN_POINT('Ctrl Pts',(-19.9707522614864,21.4524378964647,
1.9690957105548));
#130759=CARTESIAN_POINT('Ctrl Pts',(-19.8971219781181,21.493064683231,1.97326527742773));
#130760=CARTESIAN_POINT('Ctrl Pts',(-19.8214864174478,21.5300603129432,
1.97743484430066));
#130761=CARTESIAN_POINT('Ctrl Pts',(-19.7442411220081,21.5632357185035,
1.98160441117359));
#130762=CARTESIAN_POINT('Ctrl Pts',(-19.6642800151963,21.5975775141098,
1.98592057282703));
#130763=CARTESIAN_POINT('Ctrl Pts',(-19.5825943571934,21.6278252448874,
1.99023673448046));
#130764=CARTESIAN_POINT('Ctrl Pts',(-19.4996442824007,21.653823946343,1.9945528961339));
#130765=CARTESIAN_POINT('Ctrl Pts',(-19.4193962595356,21.6789757547542,
1.99872846125449));
#130766=CARTESIAN_POINT('Ctrl Pts',(-19.3379653982308,21.7001510303436,
2.00290402637507));
#130767=CARTESIAN_POINT('Ctrl Pts',(-19.2557808536483,21.7172611078589,
2.00707959149566));
#130768=CARTESIAN_POINT('Ctrl Pts',(-19.1694454234894,21.7352353621403,
2.01146605141552));
#130769=CARTESIAN_POINT('Ctrl Pts',(-19.0822787502276,21.7487228765315,
2.01585251133538));
#130770=CARTESIAN_POINT('Ctrl Pts',(-18.9947846789878,21.7576824205631,
2.02023897125524));
#130771=CARTESIAN_POINT('Ctrl Pts',(-18.907290607748,21.7666419645947,2.0246254311751));
#130772=CARTESIAN_POINT('Ctrl Pts',(-18.8194697218411,21.7710735849931,
2.02901189109496));
#130773=CARTESIAN_POINT('Ctrl Pts',(-18.7318236815475,21.7709990749291,
2.03339835101482));
#130774=CARTESIAN_POINT('Ctrl Pts',(-18.6482103252724,21.7709279931495,
2.03758298542427));
#130775=CARTESIAN_POINT('Ctrl Pts',(-18.5644448542258,21.7667560675599,
2.04176761983373));
#130776=CARTESIAN_POINT('Ctrl Pts',(-18.4809627381372,21.7584638651233,
2.04595225424318));
#130777=CARTESIAN_POINT('Ctrl Pts',(-18.3975994484511,21.7501834656048,
2.05013093234635));
#130778=CARTESIAN_POINT('Ctrl Pts',(-18.3145191664661,21.7377944834636,
2.05430961044952));
#130779=CARTESIAN_POINT('Ctrl Pts',(-18.232157552723,21.7213294919414,2.05848828855269));
#130780=CARTESIAN_POINT('Ctrl Pts',(-18.1483196667192,21.7045693773741,
2.06274186643367));
#130781=CARTESIAN_POINT('Ctrl Pts',(-18.0652269487603,21.6835856916693,
2.06699544431465));
#130782=CARTESIAN_POINT('Ctrl Pts',(-17.9833337046586,21.6584681025579,
2.07124902219563));
#130783=CARTESIAN_POINT('Ctrl Pts',(-17.9030281203093,21.6338374667446,
2.07542013619965));
#130784=CARTESIAN_POINT('Ctrl Pts',(-17.8238763766489,21.6052319257642,
2.07959125020367));
#130785=CARTESIAN_POINT('Ctrl Pts',(-17.7462950293383,21.57278722389,2.08376236420769));
#130786=CARTESIAN_POINT('Ctrl Pts',(-17.6687397151515,21.5403534091294,
2.08793207855663));
#130787=CARTESIAN_POINT('Ctrl Pts',(-17.592754174823,21.5040831693336,2.09210179290557));
#130788=CARTESIAN_POINT('Ctrl Pts',(-17.5187361779587,21.4641608559616,
2.09627150725451));
#130789=CARTESIAN_POINT('Ctrl Pts',(-17.4447208149285,21.4242399631732,
2.1004410732296));
#130790=CARTESIAN_POINT('Ctrl Pts',(-17.3726732606489,21.3806674743246,
2.10461063920469));
#130791=CARTESIAN_POINT('Ctrl Pts',(-17.3029665901884,21.3336736395411,
2.10878020517978));
#130792=CARTESIAN_POINT('Ctrl Pts',(-17.2308091202126,21.2850275601913,
2.11309636788948));
#130793=CARTESIAN_POINT('Ctrl Pts',(-17.1611606450012,21.2327153644064,
2.11741253059919));
#130794=CARTESIAN_POINT('Ctrl Pts',(-17.0944005275883,21.1770400733625,
2.12172869330889));
#130795=CARTESIAN_POINT('Ctrl Pts',(-17.0298151129693,21.1231783982271,
2.12590425753753));
#130796=CARTESIAN_POINT('Ctrl Pts',(-16.9679330839598,21.06616972251,2.13007982176617));
#130797=CARTESIAN_POINT('Ctrl Pts',(-16.9090612874293,21.006326904873,2.13425538599481));
#130798=CARTESIAN_POINT('Ctrl Pts',(-16.8472160178363,20.9434615702293,
2.13864184794505));
#130799=CARTESIAN_POINT('Ctrl Pts',(-16.7886934533832,20.8774687014113,
2.14302830989529));
#130800=CARTESIAN_POINT('Ctrl Pts',(-16.733800984635,20.8087496358731,2.14741477184553));
#130801=CARTESIAN_POINT('Ctrl Pts',(-16.6789085158868,20.740030570335,2.15180123379577));
#130802=CARTESIAN_POINT('Ctrl Pts',(-16.6276464192901,20.6685858238429,
2.156187695746));
#130803=CARTESIAN_POINT('Ctrl Pts',(-16.5802679097319,20.5948490103148,
2.16057415769624));
#130804=CARTESIAN_POINT('Ctrl Pts',(-16.5350693576789,20.5245049400697,
2.16475879184019));
#130805=CARTESIAN_POINT('Ctrl Pts',(-16.4932366287838,20.4518132565164,
2.16894342598413));
#130806=CARTESIAN_POINT('Ctrl Pts',(-16.4550217746911,20.3771296019601,
2.17312806012807));
#130807=CARTESIAN_POINT('Ctrl Pts',(-16.4168613147564,20.3025522504266,
2.17730673795853));
#130808=CARTESIAN_POINT('Ctrl Pts',(-16.3823087086574,20.225988965771,2.18148541578898));
#130809=CARTESIAN_POINT('Ctrl Pts',(-16.3515723822765,20.1478237007615,
2.18566409361943));
#130810=CARTESIAN_POINT('Ctrl Pts',(-16.320285126975,20.0682573735512,2.18991767156769));
#130811=CARTESIAN_POINT('Ctrl Pts',(-16.2929525719373,19.9870314754766,
2.19417124951595));
#130812=CARTESIAN_POINT('Ctrl Pts',(-16.2697452279946,19.904576541305,2.19842482746421));
#130813=CARTESIAN_POINT('Ctrl Pts',(-16.2469878054675,19.8237201632108,
2.20259594117976));
#130814=CARTESIAN_POINT('Ctrl Pts',(-16.2281972006316,19.74168244169,2.20676705489531));
#130815=CARTESIAN_POINT('Ctrl Pts',(-16.2134847477526,19.6588871098706,
2.21093816861085));
#130816=CARTESIAN_POINT('Ctrl Pts',(-16.1987772317894,19.5761195608809,
2.21510788266606));
#130817=CARTESIAN_POINT('Ctrl Pts',(-16.1881452304063,19.492595359046,2.21927759672127));
#130818=CARTESIAN_POINT('Ctrl Pts',(-16.1816490383843,19.408748751549,2.22344731077647));
#130819=CARTESIAN_POINT('Ctrl Pts',(-16.1751530775285,19.3249051277229,
2.22761687645293));
#130820=CARTESIAN_POINT('Ctrl Pts',(-16.1727926681034,19.2407395797697,
2.2317864421294));
#130821=CARTESIAN_POINT('Ctrl Pts',(-16.1745761446913,19.1566904347585,
2.23595600780586));
#130822=CARTESIAN_POINT('Ctrl Pts',(-16.1764223263664,19.0696862136876,
2.24027217085351));
#130823=CARTESIAN_POINT('Ctrl Pts',(-16.1827092038737,18.9828072606513,
2.24458833390116));
#130824=CARTESIAN_POINT('Ctrl Pts',(-16.1933873263915,18.896536579711,2.24890449694881));
#130825=CARTESIAN_POINT('Ctrl Pts',(-16.2037176087823,18.8130761685133,
2.25308006086957));
#130826=CARTESIAN_POINT('Ctrl Pts',(-16.2181573115163,18.7301854648529,
2.25725562479034));
#130827=CARTESIAN_POINT('Ctrl Pts',(-16.2366094603928,18.6482918228064,
2.2614311887111));
#130828=CARTESIAN_POINT('Ctrl Pts',(-16.2559935873461,18.5622619102627,
2.2658176513222));
#130829=CARTESIAN_POINT('Ctrl Pts',(-16.2798059943656,18.4773329921969,
2.27020411393329));
#130830=CARTESIAN_POINT('Ctrl Pts',(-16.3078756047625,18.3939807720541,
2.27459057654439));
#130831=CARTESIAN_POINT('Ctrl Pts',(-16.3359452151593,18.3106285519114,
2.27897703915549));
#130832=CARTESIAN_POINT('Ctrl Pts',(-16.3682717448907,18.2288535413148,
2.28336350176658));
#130833=CARTESIAN_POINT('Ctrl Pts',(-16.4046276535509,18.1491033611513,
2.28774996437768));
#130834=CARTESIAN_POINT('Ctrl Pts',(-16.4393112999297,18.0730214490394,
2.29193466292225));
#130835=CARTESIAN_POINT('Ctrl Pts',(-16.4777908907348,17.9984989913647,
2.29611936146682));
#130836=CARTESIAN_POINT('Ctrl Pts',(-16.5199038099004,17.925940444576,2.30030406001139));
#130837=CARTESIAN_POINT('Ctrl Pts',(-16.5619476212562,17.8535009672404,
2.30448189141503));
#130838=CARTESIAN_POINT('Ctrl Pts',(-16.6076126789151,17.7830193882166,
2.30865972281866));
#130839=CARTESIAN_POINT('Ctrl Pts',(-16.6566890878976,17.7148785562462,
2.3128375542223));
#130840=CARTESIAN_POINT('Ctrl Pts',(-16.7057182446351,17.6468033323214,
2.31701136308401));
#130841=CARTESIAN_POINT('Ctrl Pts',(-16.7581519651251,17.581064752514,2.32118517194572));
#130842=CARTESIAN_POINT('Ctrl Pts',(-16.8137358428997,17.518018734021,2.32535898080743));
#130843=CARTESIAN_POINT('Ctrl Pts',(-16.8692865796241,17.4550103057672,
2.32953030109846));
#130844=CARTESIAN_POINT('Ctrl Pts',(-16.9279834436642,17.3946915976913,
2.33370162138948));
#130845=CARTESIAN_POINT('Ctrl Pts',(-16.989531117982,17.337386293904,2.33787294168051));
#130846=CARTESIAN_POINT('Ctrl Pts',(-17.0486441689456,17.2823477992604,
2.34187925827464));
#130847=CARTESIAN_POINT('Ctrl Pts',(-17.1103864544927,17.2300890910807,
2.34588557486876));
#130848=CARTESIAN_POINT('Ctrl Pts',(-17.174464231106,17.180864983421,2.34989189146289));
#130849=CARTESIAN_POINT('Ctrl Pts',(-17.1739275293697,17.1801545964506,
1.55000082814524));
#130850=CARTESIAN_POINT('Ctrl Pts',(-17.7189175982832,16.7702008098065,
1.583957529087));
#130851=CARTESIAN_POINT('Ctrl Pts',(-19.3278236760405,16.3317553949947,
1.66030616558923));
#130852=CARTESIAN_POINT('Ctrl Pts',(-21.0477248457009,17.6266607733557,
1.75473569409313));
#130853=CARTESIAN_POINT('Ctrl Pts',(-21.2914432046423,18.8451666090485,
1.81520852165527));
#130854=CARTESIAN_POINT('Ctrl Pts',(-21.2901594433486,19.2099805605233,
1.83328941365693));
#130855=CARTESIAN_POINT('',(-21.2939995273705,19.2125555907563,1.76670989019937));
#130856=CARTESIAN_POINT('Ctrl Pts',(-17.174464231106,17.180864983421,1.4832495057092));
#130857=CARTESIAN_POINT('Ctrl Pts',(-17.2411722071231,17.1296203746538,
1.4874243808177));
#130858=CARTESIAN_POINT('Ctrl Pts',(-17.3103683086997,17.0816980612811,
1.49159925592621));
#130859=CARTESIAN_POINT('Ctrl Pts',(-17.381681384701,17.0373315886006,1.49577413103471));
#130860=CARTESIAN_POINT('Ctrl Pts',(-17.4530395947168,16.992937036399,1.49995164841983));
#130861=CARTESIAN_POINT('Ctrl Pts',(-17.5265170440586,16.9521030273264,
1.50412916580495));
#130862=CARTESIAN_POINT('Ctrl Pts',(-17.6017183868702,16.9150169102173,
1.50830668319008));
#130863=CARTESIAN_POINT('Ctrl Pts',(-17.6770427439097,16.8778701277013,
1.51249103415099));
#130864=CARTESIAN_POINT('Ctrl Pts',(-17.7540962011118,16.8444836556603,
1.51667538511191));
#130865=CARTESIAN_POINT('Ctrl Pts',(-17.8324643241877,16.8149963636844,
1.52085973607283));
#130866=CARTESIAN_POINT('Ctrl Pts',(-17.8652394801244,16.8026641735702,
1.52260971744095));
#130867=CARTESIAN_POINT('Ctrl Pts',(-17.8982444142715,16.791013376961,1.52435969880908));
#130868=CARTESIAN_POINT('Ctrl Pts',(-17.9314482086486,16.7800514974195,
1.52610968017721));
#130869=CARTESIAN_POINT('Ctrl Pts',(-18.0108467907137,16.7538389000734,
1.53029432358547));
#130870=CARTESIAN_POINT('Ctrl Pts',(-18.0916786884036,16.7314715385808,
1.53447896699374));
#130871=CARTESIAN_POINT('Ctrl Pts',(-18.1735366057567,16.7131047292344,
1.538663610402));
#130872=CARTESIAN_POINT('Ctrl Pts',(-18.2552780138067,16.6947640615763,
1.5428422977598));
#130873=CARTESIAN_POINT('Ctrl Pts',(-18.3380420957822,16.6804127357782,
1.5470209851176));
#130874=CARTESIAN_POINT('Ctrl Pts',(-18.421405029143,16.6701567572566,1.5511996724754));
#130875=CARTESIAN_POINT('Ctrl Pts',(-18.5062619492397,16.6597169764711,
1.5554532480747));
#130876=CARTESIAN_POINT('Ctrl Pts',(-18.5917389394536,16.6535209329784,
1.559706823674));
#130877=CARTESIAN_POINT('Ctrl Pts',(-18.6773765359446,16.651626290805,1.5639603992733));
#130878=CARTESIAN_POINT('Ctrl Pts',(-18.7613541238536,16.6497683745839,
1.56813152309571));
#130879=CARTESIAN_POINT('Ctrl Pts',(-18.8454856660802,16.6520466005361,
1.57230264691812));
#130880=CARTESIAN_POINT('Ctrl Pts',(-18.9293330503143,16.6584630268192,
1.57647377074053));
#130881=CARTESIAN_POINT('Ctrl Pts',(-19.0131523026761,16.6648773003091,
1.58064349509743));
#130882=CARTESIAN_POINT('Ctrl Pts',(-19.0966871280817,16.6754269816346,
1.58481321945433));
#130883=CARTESIAN_POINT('Ctrl Pts',(-19.1795019710685,16.6900620805395,
1.58898294381123));
#130884=CARTESIAN_POINT('Ctrl Pts',(-19.2623138707192,16.7046966592958,
1.59315251997126));
#130885=CARTESIAN_POINT('Ctrl Pts',(-19.3444053859658,16.7234162860397,
1.59732209613129));
#130886=CARTESIAN_POINT('Ctrl Pts',(-19.4253499785112,16.7461196363287,
1.60149167229132));
#130887=CARTESIAN_POINT('Ctrl Pts',(-19.5091400540413,16.7696210880709,
1.60580782350526));
#130888=CARTESIAN_POINT('Ctrl Pts',(-19.5917005594529,16.7973914247812,
1.6101239747192));
#130889=CARTESIAN_POINT('Ctrl Pts',(-19.6725761219549,16.8292622177712,
1.61444012593315));
#130890=CARTESIAN_POINT('Ctrl Pts',(-19.7508175783492,16.8600949833538,
1.61861570068712));
#130891=CARTESIAN_POINT('Ctrl Pts',(-19.8274817539353,16.8947649658156,
1.62279127544109));
#130892=CARTESIAN_POINT('Ctrl Pts',(-19.9021790183312,16.9330716031599,
1.62696685019507));
#130893=CARTESIAN_POINT('Ctrl Pts',(-19.9806484617505,16.9733127088547,
1.631353289639));
#130894=CARTESIAN_POINT('Ctrl Pts',(-20.0569466030573,17.0175671444772,
1.63573972908293));
#130895=CARTESIAN_POINT('Ctrl Pts',(-20.130655495903,17.0655505305965,1.64012616852686));
#130896=CARTESIAN_POINT('Ctrl Pts',(-20.2043643887487,17.1135339167158,
1.64451260797079));
#130897=CARTESIAN_POINT('Ctrl Pts',(-20.275483608608,17.1652458506084,1.64889904741472));
#130898=CARTESIAN_POINT('Ctrl Pts',(-20.3436364934689,17.2203542859431,
1.65328548685865));
#130899=CARTESIAN_POINT('Ctrl Pts',(-20.4078056279229,17.2722414599601,
1.6574155251252));
#130900=CARTESIAN_POINT('Ctrl Pts',(-20.4695977832764,17.3273436084189,
1.66154556339175));
#130901=CARTESIAN_POINT('Ctrl Pts',(-20.5286666498128,17.3854119807444,
1.6656756016583));
#130902=CARTESIAN_POINT('Ctrl Pts',(-20.5888757459544,17.4446012697411,
1.66988536368084));
#130903=CARTESIAN_POINT('Ctrl Pts',(-20.6462548736576,17.5068722657662,
1.67409512570339));
#130904=CARTESIAN_POINT('Ctrl Pts',(-20.7004701683271,17.5719163910649,
1.67830488772593));
#130905=CARTESIAN_POINT('Ctrl Pts',(-20.7535207653518,17.6355631848541,
1.68242421217099));
#130906=CARTESIAN_POINT('Ctrl Pts',(-20.8035417767949,17.7018647731871,
1.68654353661605));
#130907=CARTESIAN_POINT('Ctrl Pts',(-20.850256855771,17.7704942136866,1.69066286106111));
#130908=CARTESIAN_POINT('Ctrl Pts',(-20.8969436374088,17.8390820823739,
1.69477969025368));
#130909=CARTESIAN_POINT('Ctrl Pts',(-20.9403281944971,17.9099946152069,
1.69889651944625));
#130910=CARTESIAN_POINT('Ctrl Pts',(-20.9801755816481,17.9828732734739,
1.70301334863882));
#130911=CARTESIAN_POINT('Ctrl Pts',(-21.0200115244872,18.05573100073,1.70712899546334));
#130912=CARTESIAN_POINT('Ctrl Pts',(-21.0563120879347,18.1305533171676,
1.71124464228787));
#130913=CARTESIAN_POINT('Ctrl Pts',(-21.088887451558,18.206955633204,1.71536028911239));
#130914=CARTESIAN_POINT('Ctrl Pts',(-21.1227568123705,18.2863928925596,
1.71963942253631));
#130915=CARTESIAN_POINT('Ctrl Pts',(-21.1525985841264,18.3675378137456,
1.72391855596022));
#130916=CARTESIAN_POINT('Ctrl Pts',(-21.1782545843983,18.4499352677678,
1.72819768938414));
#130917=CARTESIAN_POINT('Ctrl Pts',(-21.2029529680662,18.5292572162836,
1.73231710308656));
#130918=CARTESIAN_POINT('Ctrl Pts',(-21.2237724320015,18.6097393655103,
1.73643651678898));
#130919=CARTESIAN_POINT('Ctrl Pts',(-21.2406233770012,18.6909622649548,
1.7405559304914));
#130920=CARTESIAN_POINT('Ctrl Pts',(-21.2574836176246,18.7722299700469,
1.74467761661945));
#130921=CARTESIAN_POINT('Ctrl Pts',(-21.2703709121366,18.8542387712825,
1.74879930274751));
#130922=CARTESIAN_POINT('Ctrl Pts',(-21.279247341302,18.9365624449985,1.75292098887556));
#130923=CARTESIAN_POINT('Ctrl Pts',(-21.2881358451795,19.0189981045868,
1.75704828178227));
#130924=CARTESIAN_POINT('Ctrl Pts',(-21.2930025796067,19.1017490200354,
1.76117557468897));
#130925=CARTESIAN_POINT('Ctrl Pts',(-21.2938616787506,19.1843882419918,
1.76530286759568));
#130926=CARTESIAN_POINT('Ctrl Pts',(-21.293959303024,19.19377900214,1.76577187513024));
#130927=CARTESIAN_POINT('Ctrl Pts',(-21.2940052315681,19.2031683255366,
1.76624088266481));
#130928=CARTESIAN_POINT('Ctrl Pts',(-21.2939995273705,19.2125555907563,
1.76670989019937));
#130929=CARTESIAN_POINT('Ctrl Pts',(-21.2939995273702,19.2125555913393,
1.7667098902285));
#130930=CARTESIAN_POINT('Ctrl Pts',(-21.2939437779102,19.3043011465908,
1.77129369133236));
#130931=CARTESIAN_POINT('Ctrl Pts',(-21.2889563823285,19.3958958079181,
1.77587749243622));
#130932=CARTESIAN_POINT('Ctrl Pts',(-21.2790836672346,19.4869513123279,
1.78046129354008));
#130933=CARTESIAN_POINT('Ctrl Pts',(-21.2700706759975,19.5700776312323,
1.78464593361015));
#130934=CARTESIAN_POINT('Ctrl Pts',(-21.2569640809886,19.6529166096931,
1.78883057368023));
#130935=CARTESIAN_POINT('Ctrl Pts',(-21.2397911343996,19.7350331962428,
1.7930152137503));
#130936=CARTESIAN_POINT('Ctrl Pts',(-21.2226426310956,19.817032901329,1.79719389757114));
#130937=CARTESIAN_POINT('Ctrl Pts',(-21.2014393661311,19.8983118104412,
1.80137258139199));
#130938=CARTESIAN_POINT('Ctrl Pts',(-21.1762603200948,19.9784402445079,
1.80555126521283));
#130939=CARTESIAN_POINT('Ctrl Pts',(-21.150630001539,20.0600047838296,1.80980484167153));
#130940=CARTESIAN_POINT('Ctrl Pts',(-21.1208800342882,20.1403767226468,
1.81405841813022));
#130941=CARTESIAN_POINT('Ctrl Pts',(-21.0871481593181,20.21911395204,1.81831199458892));
#130942=CARTESIAN_POINT('Ctrl Pts',(-21.0540701851445,20.2963248406336,
1.82248311440869));
#130943=CARTESIAN_POINT('Ctrl Pts',(-21.0171634957605,20.3719633904436,
1.82665423422847));
#130944=CARTESIAN_POINT('Ctrl Pts',(-20.9766076076857,20.4456299518278,
1.83082535404824));
#130945=CARTESIAN_POINT('Ctrl Pts',(-20.9360653282555,20.5192717941858,
1.83499507423679));
#130946=CARTESIAN_POINT('Ctrl Pts',(-20.8918765036875,20.5909425596168,
1.83916479442534));
#130947=CARTESIAN_POINT('Ctrl Pts',(-20.8442669697396,20.6602664752991,
1.84333451461389));
#130948=CARTESIAN_POINT('Ctrl Pts',(-20.7966591297285,20.7295879244518,
1.84750408644471));
#130949=CARTESIAN_POINT('Ctrl Pts',(-20.7456310834599,20.7965623111441,
1.85167365827553));
#130950=CARTESIAN_POINT('Ctrl Pts',(-20.691451661047,20.8608433242779,1.85584323010635));
#130951=CARTESIAN_POINT('Ctrl Pts',(-20.6353675257683,20.9273841782754,
1.86015938594928));
#130952=CARTESIAN_POINT('Ctrl Pts',(-20.5759066466623,20.9910383508709,
1.86447554179221));
#130953=CARTESIAN_POINT('Ctrl Pts',(-20.5134108769448,21.0514610647907,
1.86879169763514));
#130954=CARTESIAN_POINT('Ctrl Pts',(-20.4529507187175,21.1099156907698,
1.87296726769975));
#130955=CARTESIAN_POINT('Ctrl Pts',(-20.3896507250023,21.1653458615584,
1.87714283776436));
#130956=CARTESIAN_POINT('Ctrl Pts',(-20.3238547775404,21.2174799491478,
1.88131840782897));
#130957=CARTESIAN_POINT('Ctrl Pts',(-20.2547359396678,21.2722469627211,
1.88570485656106));
#130958=CARTESIAN_POINT('Ctrl Pts',(-20.1828628806314,21.3233758659983,
1.89009130529315));
#130959=CARTESIAN_POINT('Ctrl Pts',(-20.1086675060193,21.3706039562602,
1.89447775402525));
#130960=CARTESIAN_POINT('Ctrl Pts',(-20.0344721314073,21.417832046522,1.89886420275734));
#130961=CARTESIAN_POINT('Ctrl Pts',(-19.9579549835793,21.4611591040721,
1.90325065148943));
#130962=CARTESIAN_POINT('Ctrl Pts',(-19.8795742651121,21.5003797420072,
1.90763710022152));
#130963=CARTESIAN_POINT('Ctrl Pts',(-19.8047997208671,21.5377958997554,
1.91182173531048));
#130964=CARTESIAN_POINT('Ctrl Pts',(-19.7280509965254,21.5716144630821,
1.91600637039945));
#130965=CARTESIAN_POINT('Ctrl Pts',(-19.6497086514407,21.6016228614477,
1.92019100548841));
#130966=CARTESIAN_POINT('Ctrl Pts',(-19.5714778164362,21.6315885467837,
1.92436968429672));
#130967=CARTESIAN_POINT('Ctrl Pts',(-19.4916582921888,21.6577546763365,
1.92854836310503));
#130968=CARTESIAN_POINT('Ctrl Pts',(-19.4106541204075,21.6799550828915,
1.93272704191334));
#130969=CARTESIAN_POINT('Ctrl Pts',(-19.3281980247988,21.7025534109181,
1.93698061962124));
#130970=CARTESIAN_POINT('Ctrl Pts',(-19.2445148260133,21.7210422324063,
1.94123419732914));
#130971=CARTESIAN_POINT('Ctrl Pts',(-19.1600508252197,21.7352980597246,
1.94548777503704));
#130972=CARTESIAN_POINT('Ctrl Pts',(-19.0772243047676,21.7492775132415,
1.94965888980437));
#130973=CARTESIAN_POINT('Ctrl Pts',(-18.9936474610422,21.7591865556584,
1.95383000457171));
#130974=CARTESIAN_POINT('Ctrl Pts',(-18.9097535041071,21.7649598089622,
1.95800111933905));
#130975=CARTESIAN_POINT('Ctrl Pts',(-18.8258876981392,21.7707311250267,
1.96217083447142));
#130976=CARTESIAN_POINT('Ctrl Pts',(-18.7417054488562,21.7723693765771,
1.9663405496038));
#130977=CARTESIAN_POINT('Ctrl Pts',(-18.6576449614606,21.769861056816,1.97051026473618));
#130978=CARTESIAN_POINT('Ctrl Pts',(-18.5735874648611,21.7673528262987,
1.97467983151386));
#130979=CARTESIAN_POINT('Ctrl Pts',(-18.4896521813381,21.7606983323727,
1.97884939829154));
#130980=CARTESIAN_POINT('Ctrl Pts',(-18.4062758155005,21.7499361667624,
1.98301896506922));
#130981=CARTESIAN_POINT('Ctrl Pts',(-18.3199680751374,21.7387956212864,
1.9873351268887));
#130982=CARTESIAN_POINT('Ctrl Pts',(-18.2342598094107,21.7232532494571,
1.99165128870818));
#130983=CARTESIAN_POINT('Ctrl Pts',(-18.1496259628381,21.7034098749385,
1.99596745052765));
#130984=CARTESIAN_POINT('Ctrl Pts',(-18.0677490202285,21.6842128881249,
2.00014301559882));
#130985=CARTESIAN_POINT('Ctrl Pts',(-17.9868780138841,21.6609909777852,
2.00431858066999));
#130986=CARTESIAN_POINT('Ctrl Pts',(-17.907427475734,21.6338862668579,2.00849414574115));
#130987=CARTESIAN_POINT('Ctrl Pts',(-17.8239641319665,21.6054125792213,
2.01288060593478));
#130988=CARTESIAN_POINT('Ctrl Pts',(-17.7420690633812,21.5726537644299,
2.01726706612841));
#130989=CARTESIAN_POINT('Ctrl Pts',(-17.6621969477251,21.5358307932265,
2.02165352632205));
#130990=CARTESIAN_POINT('Ctrl Pts',(-17.5823248320691,21.4990078220231,
2.02603998651568));
#130991=CARTESIAN_POINT('Ctrl Pts',(-17.5044761476508,21.458121031537,2.03042644670931));
#130992=CARTESIAN_POINT('Ctrl Pts',(-17.4290716121317,21.4134445288214,
2.03481290690294));
#130993=CARTESIAN_POINT('Ctrl Pts',(-17.3571365542413,21.3708236601023,
2.03899753937618));
#130994=CARTESIAN_POINT('Ctrl Pts',(-17.287157912544,21.3245955127068,2.04318217184941));
#130995=CARTESIAN_POINT('Ctrl Pts',(-17.2195204146382,21.2749650155761,
2.04736680432265));
#130996=CARTESIAN_POINT('Ctrl Pts',(-17.1519791909019,21.2254051617284,
2.05154548045468));
#130997=CARTESIAN_POINT('Ctrl Pts',(-17.0867728595891,21.1724528473982,
2.0557241565867));
#130998=CARTESIAN_POINT('Ctrl Pts',(-17.0242598410811,21.1163578637568,
2.05990283271872));
#130999=CARTESIAN_POINT('Ctrl Pts',(-16.9606262846793,21.0592573846791,
2.06415641108813));
#131000=CARTESIAN_POINT('Ctrl Pts',(-16.8997839641052,20.9989007054076,
2.06840998945753));
#131001=CARTESIAN_POINT('Ctrl Pts',(-16.8420782881025,20.9355962530548,
2.07266356782693));
#131002=CARTESIAN_POINT('Ctrl Pts',(-16.7854913830301,20.8735191181162,
2.07683467978818));
#131003=CARTESIAN_POINT('Ctrl Pts',(-16.7319209084704,20.8086078458258,
2.08100579174944));
#131004=CARTESIAN_POINT('Ctrl Pts',(-16.6816563254009,20.7411913087366,
2.08517690371069));
#131005=CARTESIAN_POINT('Ctrl Pts',(-16.6314086093446,20.6737973942486,
2.08934661599456));
#131006=CARTESIAN_POINT('Ctrl Pts',(-16.5844648563589,20.6039002530621,
2.09351632827843));
#131007=CARTESIAN_POINT('Ctrl Pts',(-16.5410736157513,20.5318610348049,
2.0976860405623));
#131008=CARTESIAN_POINT('Ctrl Pts',(-16.4976839193695,20.4598243803099,
2.10185560445267));
#131009=CARTESIAN_POINT('Ctrl Pts',(-16.4578467206233,20.3856461948251,
2.10602516834305));
#131010=CARTESIAN_POINT('Ctrl Pts',(-16.421765949993,20.3097145662038,2.11019473223343));
#131011=CARTESIAN_POINT('Ctrl Pts',(-16.3844165850417,20.2311131932513,
2.11451089734601));
#131012=CARTESIAN_POINT('Ctrl Pts',(-16.3510929497969,20.1506332533461,
2.11882706245858));
#131013=CARTESIAN_POINT('Ctrl Pts',(-16.3219673468085,20.068728675012,2.12314322757116));
#131014=CARTESIAN_POINT('Ctrl Pts',(-16.2937905367765,19.989492212667,2.12731878968715));
#131015=CARTESIAN_POINT('Ctrl Pts',(-16.2695425396132,19.908922969202,2.13149435180313));
#131016=CARTESIAN_POINT('Ctrl Pts',(-16.2493282307314,19.827446428329,2.13566991391912));
#131017=CARTESIAN_POINT('Ctrl Pts',(-16.2280929123458,19.7418545687945,
2.14005638053));
#131018=CARTESIAN_POINT('Ctrl Pts',(-16.2113095991637,19.6552619180468,
2.14444284714087));
#131019=CARTESIAN_POINT('Ctrl Pts',(-16.1990385985768,19.5681703981218,
2.14882931375175));
#131020=CARTESIAN_POINT('Ctrl Pts',(-16.1867675979899,19.4810788781968,
2.15321578036263));
#131021=CARTESIAN_POINT('Ctrl Pts',(-16.1790088854247,19.3934890737652,
2.1576022469735));
#131022=CARTESIAN_POINT('Ctrl Pts',(-16.175759706546,19.3059031134812,2.16198871358438));
#131023=CARTESIAN_POINT('Ctrl Pts',(-16.1726599323334,19.222344555702,2.16617348044157));
#131024=CARTESIAN_POINT('Ctrl Pts',(-16.1736525434566,19.1384784652832,
2.17035824729877));
#131025=CARTESIAN_POINT('Ctrl Pts',(-16.1787734748956,19.0547393030766,
2.17454301415596));
#131026=CARTESIAN_POINT('Ctrl Pts',(-16.1838870736907,18.9711200466848,
2.17872178886007));
#131027=CARTESIAN_POINT('Ctrl Pts',(-16.1931172227512,18.8876278127959,
2.18290056356417));
#131028=CARTESIAN_POINT('Ctrl Pts',(-16.2064478895021,18.8046992139839,
2.18707933826827));
#131029=CARTESIAN_POINT('Ctrl Pts',(-16.219762654119,18.7218695405828,2.19125312811781));
#131030=CARTESIAN_POINT('Ctrl Pts',(-16.2371681394967,18.6396026174132,
2.19542691796735));
#131031=CARTESIAN_POINT('Ctrl Pts',(-16.258596457945,18.558330631957,2.19960070781689));
#131032=CARTESIAN_POINT('Ctrl Pts',(-16.2800107741408,18.4771117533682,
2.20377177031945));
#131033=CARTESIAN_POINT('Ctrl Pts',(-16.3054425870164,18.3968869651317,
2.20794283282201));
#131034=CARTESIAN_POINT('Ctrl Pts',(-16.3347730132237,18.3180779060164,
2.21211389532456));
#131035=CARTESIAN_POINT('Ctrl Pts',(-16.3640930721629,18.2392967031153,
2.21628348350409));
#131036=CARTESIAN_POINT('Ctrl Pts',(-16.3973088466592,18.1619306659659,
2.22045307168362));
#131037=CARTESIAN_POINT('Ctrl Pts',(-16.4342521396892,18.0863846084123,
2.22462265986315));
#131038=CARTESIAN_POINT('Ctrl Pts',(-16.471193456534,18.0108425919983,2.22879202500141));
#131039=CARTESIAN_POINT('Ctrl Pts',(-16.5118616920895,17.9371207741401,
2.23296139013968));
#131040=CARTESIAN_POINT('Ctrl Pts',(-16.5560418071037,17.865601133494,2.23713075527795));
#131041=CARTESIAN_POINT('Ctrl Pts',(-16.6002584544325,17.794022353617,2.24130356804326));
#131042=CARTESIAN_POINT('Ctrl Pts',(-16.6479925391717,17.7246497800717,
2.24547638080857));
#131043=CARTESIAN_POINT('Ctrl Pts',(-16.698984937016,17.6578375186645,2.24964919357389));
#131044=CARTESIAN_POINT('Ctrl Pts',(-16.749999304179,17.590996472185,2.25382380413372));
#131045=CARTESIAN_POINT('Ctrl Pts',(-16.8042744849681,17.5267182878878,
2.25799841469355));
#131046=CARTESIAN_POINT('Ctrl Pts',(-16.8615116627756,17.4653232180731,
2.26217302525338));
#131047=CARTESIAN_POINT('Ctrl Pts',(-16.9188352980411,17.4038354102537,
2.26635394161358));
#131048=CARTESIAN_POINT('Ctrl Pts',(-16.979129537148,17.3452397369253,2.27053485797377));
#131049=CARTESIAN_POINT('Ctrl Pts',(-17.0420596615868,17.2898186209392,
2.27471577433397));
#131050=CARTESIAN_POINT('Ctrl Pts',(-17.0850057301622,17.2519970042032,
2.27756900118382));
#131051=CARTESIAN_POINT('Ctrl Pts',(-17.1291786767271,17.2156530350981,
2.28042222803368));
#131052=CARTESIAN_POINT('Ctrl Pts',(-17.174464231106,17.180864983421,2.28327545488353));
#131053=CARTESIAN_POINT('Origin',(-18.734,19.211,-1.76670989022852));
#131054=CARTESIAN_POINT('',(-17.174464231106,17.180864983421,3.1498113662728));
#131055=CARTESIAN_POINT('',(-17.1746506278754,17.1811162280174,3.08342410660672));
#131056=CARTESIAN_POINT('',(-17.174464231106,17.180864983421,-1.76670989022852));
#131057=CARTESIAN_POINT('',(-21.2939989850552,19.2132795868247,2.63329010980608));
#131058=CARTESIAN_POINT('Ctrl Pts',(-21.2939989850552,19.2132795868247,
2.63329010980608));
#131059=CARTESIAN_POINT('Ctrl Pts',(-21.293907125607,19.3164386732131,2.63841342883254));
#131060=CARTESIAN_POINT('Ctrl Pts',(-21.2875761055109,19.4193213099601,
2.643536747859));
#131061=CARTESIAN_POINT('Ctrl Pts',(-21.2751280763078,19.5212710102476,
2.64866006688546));
#131062=CARTESIAN_POINT('Ctrl Pts',(-21.2624749613816,19.6249003682273,
2.6538677944211));
#131063=CARTESIAN_POINT('Ctrl Pts',(-21.2435016684883,19.7275658815507,
2.65907552195674));
#131064=CARTESIAN_POINT('Ctrl Pts',(-21.2183850428165,19.8286009707164,
2.66428324949238));
#131065=CARTESIAN_POINT('Ctrl Pts',(-21.2103562166331,19.8608980308362,
2.66594796113558));
#131066=CARTESIAN_POINT('Ctrl Pts',(-21.2017000059957,19.8930286552932,
2.66761267277878));
#131067=CARTESIAN_POINT('Ctrl Pts',(-21.1924232051054,19.9249715292638,
2.66927738442198));
#131068=CARTESIAN_POINT('Ctrl Pts',(-21.1691038390111,20.0052672670978,
2.67346201883512));
#131069=CARTESIAN_POINT('Ctrl Pts',(-21.1418030734501,20.0845687630516,
2.67764665324825));
#131070=CARTESIAN_POINT('Ctrl Pts',(-21.1106233366689,20.1624523191421,
2.68183128766138));
#131071=CARTESIAN_POINT('Ctrl Pts',(-21.0794879803815,20.240225017636,2.68600996576567));
#131072=CARTESIAN_POINT('Ctrl Pts',(-21.0444847892983,20.3165833617425,
2.69018864386997));
#131073=CARTESIAN_POINT('Ctrl Pts',(-21.0057661997906,20.3911179320259,
2.69436732197426));
#131074=CARTESIAN_POINT('Ctrl Pts',(-20.9663536076312,20.4669884804549,
2.69862089985464));
#131075=CARTESIAN_POINT('Ctrl Pts',(-20.923091244407,20.5409687666864,2.70287447773502));
#131076=CARTESIAN_POINT('Ctrl Pts',(-20.8761915739271,20.6126473381689,
2.7071280556154));
#131077=CARTESIAN_POINT('Ctrl Pts',(-20.8302011447919,20.6829362811089,
2.71129916961421));
#131078=CARTESIAN_POINT('Ctrl Pts',(-20.7807134458812,20.7510115566354,
2.71547028361302));
#131079=CARTESIAN_POINT('Ctrl Pts',(-20.7279747027012,20.8165107863192,
2.71964139761183));
#131080=CARTESIAN_POINT('Ctrl Pts',(-20.675253656514,20.8819880371064,2.72381111195321));
#131081=CARTESIAN_POINT('Ctrl Pts',(-20.6192840209112,20.9448906007769,
2.72798082629458));
#131082=CARTESIAN_POINT('Ctrl Pts',(-20.560353487436,21.0048876606215,2.73215054063596));
#131083=CARTESIAN_POINT('Ctrl Pts',(-20.5014250509605,21.0648825855149,
2.73632010660112));
#131084=CARTESIAN_POINT('Ctrl Pts',(-20.4395362490684,21.1219718845495,
2.74048967256628));
#131085=CARTESIAN_POINT('Ctrl Pts',(-20.3750119946268,21.1758612249955,
2.74465923853145));
#131086=CARTESIAN_POINT('Ctrl Pts',(-20.3082191477172,21.2316452475716,
2.74897540124578));
#131087=CARTESIAN_POINT('Ctrl Pts',(-20.2386024799585,21.2839997657249,
2.75329156396011));
#131088=CARTESIAN_POINT('Ctrl Pts',(-20.1665585536104,21.3326446428367,
2.75760772667444));
#131089=CARTESIAN_POINT('Ctrl Pts',(-20.0968614498344,21.3797049187001,
2.76178329088732));
#131090=CARTESIAN_POINT('Ctrl Pts',(-20.0248932222208,21.4232933214429,
2.76595885510019));
#131091=CARTESIAN_POINT('Ctrl Pts',(-19.9510397173094,21.463202106049,2.77013441931307));
#131092=CARTESIAN_POINT('Ctrl Pts',(-19.8734560486687,21.5051265878247,
2.77452088127813));
#131093=CARTESIAN_POINT('Ctrl Pts',(-19.7937921742969,21.5429897170771,
2.77890734324319));
#131094=CARTESIAN_POINT('Ctrl Pts',(-19.7125190809761,21.5766078305936,
2.78329380520824));
#131095=CARTESIAN_POINT('Ctrl Pts',(-19.6312459876554,21.61022594411,2.7876802671733));
#131096=CARTESIAN_POINT('Ctrl Pts',(-19.5483642476832,21.6395989197709,
2.79206672913836));
#131097=CARTESIAN_POINT('Ctrl Pts',(-19.4643607861727,21.6646041086575,
2.79645319110342));
#131098=CARTESIAN_POINT('Ctrl Pts',(-19.3842224476358,21.6884587719791,
2.80063782549364));
#131099=CARTESIAN_POINT('Ctrl Pts',(-19.3027650531594,21.7084275441982,
2.80482245988387));
#131100=CARTESIAN_POINT('Ctrl Pts',(-19.2204003081572,21.7243672115758,
2.80900709427409));
#131101=CARTESIAN_POINT('Ctrl Pts',(-19.1381527991746,21.7402841908099,
2.81318577235522));
#131102=CARTESIAN_POINT('Ctrl Pts',(-19.0550009527839,21.7521833699235,
2.81736445043635));
#131103=CARTESIAN_POINT('Ctrl Pts',(-18.97137153685,21.7599713128032,2.82154312851748));
#131104=CARTESIAN_POINT('Ctrl Pts',(-18.8862431236674,21.7678988489685,
2.82579670640362));
#131105=CARTESIAN_POINT('Ctrl Pts',(-18.8006203137736,21.7715661738213,
2.83005028428976));
#131106=CARTESIAN_POINT('Ctrl Pts',(-18.7149640762858,21.7709292243358,
2.8343038621759));
#131107=CARTESIAN_POINT('Ctrl Pts',(-18.630968452176,21.7703046233594,2.83847497615107));
#131108=CARTESIAN_POINT('Ctrl Pts',(-18.5469411662298,21.7655411558157,
2.84264609012625));
#131109=CARTESIAN_POINT('Ctrl Pts',(-18.4633201985508,21.7566497098162,
2.84681720410142));
#131110=CARTESIAN_POINT('Ctrl Pts',(-18.3797272906949,21.7477612474273,
2.85098691841903));
#131111=CARTESIAN_POINT('Ctrl Pts',(-18.2965408873982,21.734747606179,2.85515663273665));
#131112=CARTESIAN_POINT('Ctrl Pts',(-18.2141948751329,21.7176716243182,
2.85932634705426));
#131113=CARTESIAN_POINT('Ctrl Pts',(-18.1318517930915,21.7005962500939,
2.86349591299557));
#131114=CARTESIAN_POINT('Ctrl Pts',(-18.0503494928999,21.6794589169143,
2.86766547893688));
#131115=CARTESIAN_POINT('Ctrl Pts',(-17.9701113309735,21.6543735083554,
2.87183504487819));
#131116=CARTESIAN_POINT('Ctrl Pts',(-17.8870520941402,21.6284061277408,
2.87615120762041));
#131117=CARTESIAN_POINT('Ctrl Pts',(-17.8053480471357,21.5982080349101,
2.88046737036263));
#131118=CARTESIAN_POINT('Ctrl Pts',(-17.7254493921661,21.5639610433319,
2.88478353310486));
#131119=CARTESIAN_POINT('Ctrl Pts',(-17.6481534275864,21.5308296439486,
2.88895909729389));
#131120=CARTESIAN_POINT('Ctrl Pts',(-17.572547442585,21.4939093297973,2.89313466148293));
#131121=CARTESIAN_POINT('Ctrl Pts',(-17.4990149692544,21.4534120883179,
2.89731022567196));
#131122=CARTESIAN_POINT('Ctrl Pts',(-17.4217685453432,21.4108694273566,
2.90169668769078));
#131123=CARTESIAN_POINT('Ctrl Pts',(-17.3468111003271,21.3643793093811,
2.90608314970959));
#131124=CARTESIAN_POINT('Ctrl Pts',(-17.2745520021318,21.3142383463408,
2.91046961172841));
#131125=CARTESIAN_POINT('Ctrl Pts',(-17.2022929039366,21.2640973833005,
2.91485607374722));
#131126=CARTESIAN_POINT('Ctrl Pts',(-17.1327325650194,21.210305990306,2.91924253576604));
#131127=CARTESIAN_POINT('Ctrl Pts',(-17.0662376770537,21.1532072068038,
2.92362899778485));
#131128=CARTESIAN_POINT('Ctrl Pts',(-17.002802317601,21.0987356230989,2.92781363217408));
#131129=CARTESIAN_POINT('Ctrl Pts',(-16.9419203976439,21.0410515629429,
2.9319982665633));
#131130=CARTESIAN_POINT('Ctrl Pts',(-16.8839351856049,20.9804236865537,
2.93618290095253));
#131131=CARTESIAN_POINT('Ctrl Pts',(-16.8260325083393,20.9198821064435,
2.94036157903258));
#131132=CARTESIAN_POINT('Ctrl Pts',(-16.7710186644538,20.8564053626863,
2.94454025711262));
#131133=CARTESIAN_POINT('Ctrl Pts',(-16.7192032202845,20.7903017243225,
2.94871893519267));
#131134=CARTESIAN_POINT('Ctrl Pts',(-16.6664590214563,20.7230132256708,
2.95297251307907));
#131135=CARTESIAN_POINT('Ctrl Pts',(-16.6170293785849,20.6530030460409,
2.95722609096547));
#131136=CARTESIAN_POINT('Ctrl Pts',(-16.5712008555424,20.5806349370301,
2.96147966885187));
#131137=CARTESIAN_POINT('Ctrl Pts',(-16.5262608079,20.5096698251122,2.96565078282577));
#131138=CARTESIAN_POINT('Ctrl Pts',(-16.4847837540961,20.4364378006271,
2.96982189679967));
#131139=CARTESIAN_POINT('Ctrl Pts',(-16.4469976092755,20.3613130290578,
2.97399301077356));
#131140=CARTESIAN_POINT('Ctrl Pts',(-16.4092241439611,20.2862134663322,
2.97816272508983));
#131141=CARTESIAN_POINT('Ctrl Pts',(-16.3751393344488,20.2092228285331,
2.98233243940609));
#131142=CARTESIAN_POINT('Ctrl Pts',(-16.3449251982356,20.1307399586701,
2.98650215372236));
#131143=CARTESIAN_POINT('Ctrl Pts',(-16.3147121371714,20.0522598815654,
2.99067171966225));
#131144=CARTESIAN_POINT('Ctrl Pts',(-16.2883696400355,19.972288107597,2.99484128560214));
#131145=CARTESIAN_POINT('Ctrl Pts',(-16.2660311035614,19.8912422555324,
2.99901085154203));
#131146=CARTESIAN_POINT('Ctrl Pts',(-16.2429071716539,19.8073469311138,
3.00332701428572));
#131147=CARTESIAN_POINT('Ctrl Pts',(-16.2240741377499,19.7223011025938,
3.00764317702941));
#131148=CARTESIAN_POINT('Ctrl Pts',(-16.2096228114109,19.6365817309647,
3.0119593397731));
#131149=CARTESIAN_POINT('Ctrl Pts',(-16.1956422355369,19.5536546590259,
3.01613490396055));
#131150=CARTESIAN_POINT('Ctrl Pts',(-16.1857622912647,19.4700977247645,
3.02031046814801));
#131151=CARTESIAN_POINT('Ctrl Pts',(-16.1800123293527,19.3863481627553,
3.02448603233547));
#131152=CARTESIAN_POINT('Ctrl Pts',(-16.173971950515,19.29836860919,3.02887249435727));
#131153=CARTESIAN_POINT('Ctrl Pts',(-16.1724897391971,19.2101770410221,
3.03325895637908));
#131154=CARTESIAN_POINT('Ctrl Pts',(-16.175537874784,19.1222782223174,3.03764541840088));
#131155=CARTESIAN_POINT('Ctrl Pts',(-16.1785860103709,19.0343794036126,
3.04203188042268));
#131156=CARTESIAN_POINT('Ctrl Pts',(-16.1861643670755,18.9467739058737,
3.04641834244449));
#131157=CARTESIAN_POINT('Ctrl Pts',(-16.1981829862585,18.8599557395154,
3.05080480446629));
#131158=CARTESIAN_POINT('Ctrl Pts',(-16.2096452990133,18.7771561299727,
3.05498823010074));
#131159=CARTESIAN_POINT('Ctrl Pts',(-16.2251885633081,18.6947644704974,
3.05917165573519));
#131160=CARTESIAN_POINT('Ctrl Pts',(-16.2447727253535,18.6132144404924,
3.06335508136964));
#131161=CARTESIAN_POINT('Ctrl Pts',(-16.2643314314933,18.5317704109307,
3.06753306929951));
#131162=CARTESIAN_POINT('Ctrl Pts',(-16.2879205024912,18.4511662821532,
3.07171105722938));
#131163=CARTESIAN_POINT('Ctrl Pts',(-16.3154483597582,18.3718290022387,
3.07588904515925));
#131164=CARTESIAN_POINT('Ctrl Pts',(-16.3429486961517,18.2925710394765,
3.08006285616113));
#131165=CARTESIAN_POINT('Ctrl Pts',(-16.3743798496378,18.2145778427126,
3.08423666716302));
#131166=CARTESIAN_POINT('Ctrl Pts',(-16.4095998941466,18.1382632438904,
3.08841047816491));
#131167=CARTESIAN_POINT('Ctrl Pts',(-16.4447952944457,18.0620020440062,
3.09258136866301));
#131168=CARTESIAN_POINT('Ctrl Pts',(-16.4837741268733,17.9874175251811,
3.09675225916111));
#131169=CARTESIAN_POINT('Ctrl Pts',(-16.5263461035608,17.9149042189959,
3.10092314965921));
#131170=CARTESIAN_POINT('Ctrl Pts',(-16.568912884215,17.8423997632702,3.10509353108802));
#131171=CARTESIAN_POINT('Ctrl Pts',(-16.6150717177094,17.7719664217462,
3.10926391251683));
#131172=CARTESIAN_POINT('Ctrl Pts',(-16.6645865127571,17.7039738493254,
3.11343429394564));
#131173=CARTESIAN_POINT('Ctrl Pts',(-16.7140950873173,17.6359898187343,
3.11760415145416));
#131174=CARTESIAN_POINT('Ctrl Pts',(-16.7669585097326,17.5704463163712,
3.12177400896269));
#131175=CARTESIAN_POINT('Ctrl Pts',(-16.8228985547876,17.5076822768177,
3.12594386647121));
#131176=CARTESIAN_POINT('Ctrl Pts',(-16.8788810408977,17.4448706189247,
3.13011688760165));
#131177=CARTESIAN_POINT('Ctrl Pts',(-16.9379445037493,17.3848429786151,
3.13428990873209));
#131178=CARTESIAN_POINT('Ctrl Pts',(-16.9997721933365,17.3279031053621,
3.13846292986253));
#131179=CARTESIAN_POINT('Ctrl Pts',(-17.0558185269752,17.2762875403136,
3.14224574199928));
#131180=CARTESIAN_POINT('Ctrl Pts',(-17.1141356442521,17.2272089892714,
3.14602855413604));
#131181=CARTESIAN_POINT('Ctrl Pts',(-17.174464231106,17.180864983421,3.1498113662728));
#131182=CARTESIAN_POINT('Ctrl Pts',(-17.174464231106,17.180864983421,2.34989189146289));
#131183=CARTESIAN_POINT('Ctrl Pts',(-17.241152638798,17.1296354069067,2.3540614318011));
#131184=CARTESIAN_POINT('Ctrl Pts',(-17.3103705782716,17.081693266079,2.35823097213931));
#131185=CARTESIAN_POINT('Ctrl Pts',(-17.3817556972678,17.0372853577969,
2.36240051247752));
#131186=CARTESIAN_POINT('Ctrl Pts',(-17.4566944501041,16.9906667724457,
2.36677761735932));
#131187=CARTESIAN_POINT('Ctrl Pts',(-17.5340212921428,16.9479437450928,
2.37115472224112));
#131188=CARTESIAN_POINT('Ctrl Pts',(-17.6132860861713,16.9093483488263,
2.37553182712292));
#131189=CARTESIAN_POINT('Ctrl Pts',(-17.6888992754678,16.8725309819279,
2.37970728564841));
#131190=CARTESIAN_POINT('Ctrl Pts',(-17.7662753462856,16.8394694792919,
2.3838827441739));
#131191=CARTESIAN_POINT('Ctrl Pts',(-17.8450032186746,16.8103157802841,
2.3880582026994));
#131192=CARTESIAN_POINT('Ctrl Pts',(-17.9237867859504,16.7811414569165,
2.39223661509222));
#131193=CARTESIAN_POINT('Ctrl Pts',(-18.0039236197102,16.7558805757865,
2.39641502748503));
#131194=CARTESIAN_POINT('Ctrl Pts',(-18.084988586325,16.7346348845698,2.40059343987785));
#131195=CARTESIAN_POINT('Ctrl Pts',(-18.1661798043565,16.7133561050941,
2.40477835977331));
#131196=CARTESIAN_POINT('Ctrl Pts',(-18.248301589755,16.696105081518,2.40896327966877));
#131197=CARTESIAN_POINT('Ctrl Pts',(-18.3309204231734,16.6829321894488,
2.41314819956423));
#131198=CARTESIAN_POINT('Ctrl Pts',(-18.3426180491651,16.6810670993927,
2.41374072339586));
#131199=CARTESIAN_POINT('Ctrl Pts',(-18.3543256354134,16.6792836761072,
2.41433324722749));
#131200=CARTESIAN_POINT('Ctrl Pts',(-18.3660419494175,16.6775819782335,
2.41492577105912));
#131201=CARTESIAN_POINT('Ctrl Pts',(-18.4487871282914,16.6655639241848,
2.41911040544311));
#131202=CARTESIAN_POINT('Ctrl Pts',(-18.5322757027657,16.6575816378619,
2.42329503982711));
#131203=CARTESIAN_POINT('Ctrl Pts',(-18.6160795877535,16.6537173061283,
2.4274796742111));
#131204=CARTESIAN_POINT('Ctrl Pts',(-18.6997641882883,16.6498584747925,
2.43165835228623));
#131205=CARTESIAN_POINT('Ctrl Pts',(-18.7837627522538,16.6501059764733,
2.43583703036135));
#131206=CARTESIAN_POINT('Ctrl Pts',(-18.8676394869534,16.654490565727,2.44001570843648));
#131207=CARTESIAN_POINT('Ctrl Pts',(-18.9530196520664,16.6589537456037,
2.44426928632415));
#131208=CARTESIAN_POINT('Ctrl Pts',(-19.0382731002415,16.6677038557804,
2.44852286421182));
#131209=CARTESIAN_POINT('Ctrl Pts',(-19.122937334958,16.6807178518047,2.45277644209949));
#131210=CARTESIAN_POINT('Ctrl Pts',(-19.2059601880687,16.6934795460895,
2.45694755606923));
#131211=CARTESIAN_POINT('Ctrl Pts',(-19.2884159943217,16.7103412009493,
2.46111867003897));
#131212=CARTESIAN_POINT('Ctrl Pts',(-19.3698729492393,16.7312287217516,
2.4652897840087));
#131213=CARTESIAN_POINT('Ctrl Pts',(-19.4513025704941,16.7521092335459,
2.46945949832113));
#131214=CARTESIAN_POINT('Ctrl Pts',(-19.5317335608297,16.7770128141669,
2.47362921263355));
#131215=CARTESIAN_POINT('Ctrl Pts',(-19.6107456770759,16.8058145564783,
2.47779892694598));
#131216=CARTESIAN_POINT('Ctrl Pts',(-19.6897549817366,16.8346152739018,
2.48196849288232));
#131217=CARTESIAN_POINT('Ctrl Pts',(-19.7673450807731,16.8673137188663,
2.48613805881867));
#131218=CARTESIAN_POINT('Ctrl Pts',(-19.8431135303129,16.903735997577,2.49030762475501));
#131219=CARTESIAN_POINT('Ctrl Pts',(-19.9215459053923,16.9414388388313,
2.49462378750381));
#131220=CARTESIAN_POINT('Ctrl Pts',(-19.99802567382,16.9831320175021,2.4989399502526));
#131221=CARTESIAN_POINT('Ctrl Pts',(-20.07213364893,17.028570542354,2.5032561130014));
#131222=CARTESIAN_POINT('Ctrl Pts',(-20.1438275642621,17.0725289118643,
2.50743167718612));
#131223=CARTESIAN_POINT('Ctrl Pts',(-20.2133014733533,17.1199920607243,
2.51160724137085));
#131224=CARTESIAN_POINT('Ctrl Pts',(-20.2802065216071,17.1706947795637,
2.51578280555557));
#131225=CARTESIAN_POINT('Ctrl Pts',(-20.3504907852066,17.2239583725082,
2.5201692675864));
#131226=CARTESIAN_POINT('Ctrl Pts',(-20.417939415174,17.2807970211657,2.52455572961723));
#131227=CARTESIAN_POINT('Ctrl Pts',(-20.4821902270871,17.3408580455171,
2.52894219164806));
#131228=CARTESIAN_POINT('Ctrl Pts',(-20.5464410390001,17.4009190698685,
2.53332865367889));
#131229=CARTESIAN_POINT('Ctrl Pts',(-20.6074936847495,17.4642019995335,
2.53771511570972));
#131230=CARTESIAN_POINT('Ctrl Pts',(-20.665034920053,17.5303143846823,2.54210157774055));
#131231=CARTESIAN_POINT('Ctrl Pts',(-20.7194682477108,17.5928559186633,
2.54625111891261));
#131232=CARTESIAN_POINT('Ctrl Pts',(-20.7709705307844,17.6581717364551,
2.55040066008466));
#131233=CARTESIAN_POINT('Ctrl Pts',(-20.8192426277969,17.7259534743927,
2.55455020125671));
#131234=CARTESIAN_POINT('Ctrl Pts',(-20.8674506257227,17.7936452069694,
2.55869423237604));
#131235=CARTESIAN_POINT('Ctrl Pts',(-20.912436679677,17.8637959851797,2.56283826349536));
#131236=CARTESIAN_POINT('Ctrl Pts',(-20.953940279832,17.936062686255,2.56698229461468));
#131237=CARTESIAN_POINT('Ctrl Pts',(-20.9954017278126,18.0082559913218,
2.57112211694435));
#131238=CARTESIAN_POINT('Ctrl Pts',(-21.0333875106824,18.0825605501461,
2.57526193927403));
#131239=CARTESIAN_POINT('Ctrl Pts',(-21.0676798966809,18.1586036203847,
2.5794017616037));
#131240=CARTESIAN_POINT('Ctrl Pts',(-21.1019481578681,18.2345931940623,
2.58353867155416));
#131241=CARTESIAN_POINT('Ctrl Pts',(-21.1325279904635,18.3123184247114,
2.58767558150461));
#131242=CARTESIAN_POINT('Ctrl Pts',(-21.1592478841653,18.3913825890383,
2.59181249145506));
#131243=CARTESIAN_POINT('Ctrl Pts',(-21.185962767493,18.4704319276684,2.59594862567389));
#131244=CARTESIAN_POINT('Ctrl Pts',(-21.2088189905586,18.5508192612332,
2.60008475989273));
#131245=CARTESIAN_POINT('Ctrl Pts',(-21.2276938748212,18.6321296702378,
2.60422089411156));
#131246=CARTESIAN_POINT('Ctrl Pts',(-21.2465668271893,18.7134317569063,
2.60835660498608));
#131247=CARTESIAN_POINT('Ctrl Pts',(-21.261459151574,18.7956562735645,2.61249231586059));
#131248=CARTESIAN_POINT('Ctrl Pts',(-21.272298987946,18.8783767179039,2.61662802673511));
#131249=CARTESIAN_POINT('Ctrl Pts',(-21.2831447249188,18.9611421906275,
2.62076598885936));
#131250=CARTESIAN_POINT('Ctrl Pts',(-21.2899335186437,19.0444036643965,
2.62490395098361));
#131251=CARTESIAN_POINT('Ctrl Pts',(-21.2926453380231,19.1277291514849,
2.62904191310786));
#131252=CARTESIAN_POINT('Ctrl Pts',(-21.2935733586038,19.1562442389939,
2.63045797866241));
#131253=CARTESIAN_POINT('Ctrl Pts',(-21.2940243746441,19.1847668138181,
2.63187404421695));
#131254=CARTESIAN_POINT('Ctrl Pts',(-21.2939989850559,19.2132795861284,
2.6332901097715));
#131255=CARTESIAN_POINT('',(-21.2939990581246,19.2088040034447,2.5667098902285));
#131256=CARTESIAN_POINT('Ctrl Pts',(-17.174464231106,17.180864983421,2.28327545488353));
#131257=CARTESIAN_POINT('Ctrl Pts',(-17.2056207198402,17.156930782879,2.28523847667762));
#131258=CARTESIAN_POINT('Ctrl Pts',(-17.2373037248014,17.133732871778,2.28720149847172));
#131259=CARTESIAN_POINT('Ctrl Pts',(-17.2694745299327,17.1112940330789,
2.28916452026581));
#131260=CARTESIAN_POINT('Ctrl Pts',(-17.3380540324817,17.0634604650508,
2.29334915467525));
#131261=CARTESIAN_POINT('Ctrl Pts',(-17.4091070955312,17.0189012759421,
2.29753378908469));
#131262=CARTESIAN_POINT('Ctrl Pts',(-17.4822878905536,16.977881822414,2.30171842349413));
#131263=CARTESIAN_POINT('Ctrl Pts',(-17.5553645218218,16.9369207549729,
2.30589710159728));
#131264=CARTESIAN_POINT('Ctrl Pts',(-17.6305624715266,16.8994896383272,
2.31007577970043));
#131265=CARTESIAN_POINT('Ctrl Pts',(-17.7075059667129,16.865811308311,2.31425445780358));
#131266=CARTESIAN_POINT('Ctrl Pts',(-17.78582861831,16.8315293186269,2.31850803568457));
#131267=CARTESIAN_POINT('Ctrl Pts',(-17.8659596132366,16.8011362520549,
2.32276161356556));
#131268=CARTESIAN_POINT('Ctrl Pts',(-17.9474751923745,16.7748188230368,
2.32701519144654));
#131269=CARTESIAN_POINT('Ctrl Pts',(-18.0274104335289,16.7490116085464,
2.33118630545054));
#131270=CARTESIAN_POINT('Ctrl Pts',(-18.1086765943189,16.7271235613587,
2.33535741945454));
#131271=CARTESIAN_POINT('Ctrl Pts',(-18.1908544682415,16.7092820040359,
2.33952853345854));
#131272=CARTESIAN_POINT('Ctrl Pts',(-18.2730047666344,16.6914464336092,
2.34369824780747));
#131273=CARTESIAN_POINT('Ctrl Pts',(-18.3560657213856,16.6776547538851,
2.34786796215639));
#131274=CARTESIAN_POINT('Ctrl Pts',(-18.4396056840352,16.667983683354,2.35203767650531));
#131275=CARTESIAN_POINT('Ctrl Pts',(-18.5231426740241,16.6583129569554,
2.35620724248039));
#131276=CARTESIAN_POINT('Ctrl Pts',(-18.6071581809428,16.6527626002749,
2.36037680845546));
#131277=CARTESIAN_POINT('Ctrl Pts',(-18.6912145090001,16.6513575636898,
2.36454637443054));
#131278=CARTESIAN_POINT('Ctrl Pts',(-18.7782261526212,16.6499031277724,
2.36886253714026));
#131279=CARTESIAN_POINT('Ctrl Pts',(-18.8652810139809,16.6528909431617,
2.37317869984999));
#131280=CARTESIAN_POINT('Ctrl Pts',(-18.9518945613659,16.6602899106078,
2.37749486255972));
#131281=CARTESIAN_POINT('Ctrl Pts',(-19.035686682863,16.6674478575793,2.38167042678834));
#131282=CARTESIAN_POINT('Ctrl Pts',(-19.1190653399935,16.6787338735463,
2.38584599101697));
#131283=CARTESIAN_POINT('Ctrl Pts',(-19.2015998086533,16.694067259749,2.39002155524559));
#131284=CARTESIAN_POINT('Ctrl Pts',(-19.2883028951201,16.710175098466,2.39440801719587));
#131285=CARTESIAN_POINT('Ctrl Pts',(-19.3740737042672,16.7307497815342,
2.39879447914615));
#131286=CARTESIAN_POINT('Ctrl Pts',(-19.4584303876713,16.7556383945703,
2.40318094109642));
#131287=CARTESIAN_POINT('Ctrl Pts',(-19.5427870710755,16.7805270076064,
2.4075674030467));
#131288=CARTESIAN_POINT('Ctrl Pts',(-19.6257291067111,16.8097292861734,
2.41195386499698));
#131289=CARTESIAN_POINT('Ctrl Pts',(-19.7068005673283,16.8430348279154,
2.41634032694725));
#131290=CARTESIAN_POINT('Ctrl Pts',(-19.7841418063579,16.8748079308701,
2.42052496109111));
#131291=CARTESIAN_POINT('Ctrl Pts',(-19.8600687027665,16.9104332654798,
2.42470959523496));
#131292=CARTESIAN_POINT('Ctrl Pts',(-19.9341709431984,16.949763677299,2.42889422937882));
#131293=CARTESIAN_POINT('Ctrl Pts',(-20.0081677081793,16.9890381071006,
2.43307290720919));
#131294=CARTESIAN_POINT('Ctrl Pts',(-20.0803445731189,17.0320069250119,
2.43725158503956));
#131295=CARTESIAN_POINT('Ctrl Pts',(-20.1503107695878,17.0784747823415,
2.44143026286993));
#131296=CARTESIAN_POINT('Ctrl Pts',(-20.2215310652186,17.125775546187,2.44568384081822));
#131297=CARTESIAN_POINT('Ctrl Pts',(-20.290460214072,17.1767018411764,2.4499374187665));
#131298=CARTESIAN_POINT('Ctrl Pts',(-20.3567118459902,17.2309984179595,
2.45419099671478));
#131299=CARTESIAN_POINT('Ctrl Pts',(-20.421679055696,17.2842423455132,2.45836211043023));
#131300=CARTESIAN_POINT('Ctrl Pts',(-20.4840712680033,17.3407267365035,
2.46253322414569));
#131301=CARTESIAN_POINT('Ctrl Pts',(-20.5435545162614,17.4001680219639,
2.46670433786114));
#131302=CARTESIAN_POINT('Ctrl Pts',(-20.6030178043004,17.4595893612863,
2.47087405191626));
#131303=CARTESIAN_POINT('Ctrl Pts',(-20.6595737417694,17.5219652996142,
2.47504376597137));
#131304=CARTESIAN_POINT('Ctrl Pts',(-20.7129241774329,17.5869744152349,
2.47921348002649));
#131305=CARTESIAN_POINT('Ctrl Pts',(-20.7662727146278,17.6519812175144,
2.48338304570285));
#131306=CARTESIAN_POINT('Ctrl Pts',(-20.8164156856331,17.7196206546306,
2.48755261137921));
#131307=CARTESIAN_POINT('Ctrl Pts',(-20.863095194694,17.7895381989196,2.49172217705558));
#131308=CARTESIAN_POINT('Ctrl Pts',(-20.9114159042677,17.8619139676384,
2.49603834010334));
#131309=CARTESIAN_POINT('Ctrl Pts',(-20.9560247758967,17.9367305826506,
2.5003545031511));
#131310=CARTESIAN_POINT('Ctrl Pts',(-20.9966856911894,18.0135637959011,
2.50467066619885));
#131311=CARTESIAN_POINT('Ctrl Pts',(-21.0360220760754,18.0878941651683,
2.50884623011952));
#131312=CARTESIAN_POINT('Ctrl Pts',(-21.0716636083121,18.1641113216876,
2.51302179404019));
#131313=CARTESIAN_POINT('Ctrl Pts',(-21.1034449999947,18.2418094139954,
2.51719735796086));
#131314=CARTESIAN_POINT('Ctrl Pts',(-21.1368316009424,18.3234318686752,
2.52158382057216));
#131315=CARTESIAN_POINT('Ctrl Pts',(-21.1659576673028,18.4066882444733,
2.52597028318347));
#131316=CARTESIAN_POINT('Ctrl Pts',(-21.1906909603742,18.491090613191,2.53035674579477));
#131317=CARTESIAN_POINT('Ctrl Pts',(-21.2154242534456,18.5754929819087,
2.53474320840607));
#131318=CARTESIAN_POINT('Ctrl Pts',(-21.2357647130149,18.6610407614697,
2.53912967101737));
#131319=CARTESIAN_POINT('Ctrl Pts',(-21.251642469363,18.7472367021208,2.54351613362868));
#131320=CARTESIAN_POINT('Ctrl Pts',(-21.2744558894944,18.8710844400873,
2.54981867488504));
#131321=CARTESIAN_POINT('Ctrl Pts',(-21.288135817693,18.9966631545043,2.5561212161414));
#131322=CARTESIAN_POINT('Ctrl Pts',(-21.2924829866055,19.122881856295,2.56242375739777));
#131323=CARTESIAN_POINT('Ctrl Pts',(-21.293468437957,19.1514941308042,2.56385246834134));
#131324=CARTESIAN_POINT('Ctrl Pts',(-21.2939744691008,19.18013916897,2.56528117928492));
#131325=CARTESIAN_POINT('Ctrl Pts',(-21.2939990581246,19.2088040034447,
2.5667098902285));
#131326=CARTESIAN_POINT('Ctrl Pts',(-21.2953148853665,19.2088155456687,
2.56671052144854));
#131327=CARTESIAN_POINT('Ctrl Pts',(-21.2889869060013,19.9045867976347,
2.6013709944024));
#131328=CARTESIAN_POINT('Ctrl Pts',(-20.6359184624636,21.4617758669056,
2.67842340291674));
#131329=CARTESIAN_POINT('Ctrl Pts',(-18.0006016372723,22.1479062807659,
2.79786774699155));
#131330=CARTESIAN_POINT('Ctrl Pts',(-15.8675519701989,20.1840197011935,
2.92504355367299));
#131331=CARTESIAN_POINT('Ctrl Pts',(-16.2393387098563,18.0460023819557,
3.02022900687805));
#131332=CARTESIAN_POINT('Ctrl Pts',(-17.0075187134083,17.3068569533771,
3.07302252452263));
#131333=CARTESIAN_POINT('Ctrl Pts',(-17.1746506278756,17.1811162280172,
3.08342410660674));
#131334=CARTESIAN_POINT('Origin',(-18.734,19.211,-1.76670989022852));
#131335=CARTESIAN_POINT('',(-17.174464231106,17.180864983421,3.94993168719587));
#131336=CARTESIAN_POINT('',(-17.174464231106,17.180864983421,3.88329345071054));
#131337=CARTESIAN_POINT('',(-17.174464231106,17.180864983421,-1.76670989022852));
#131338=CARTESIAN_POINT('',(-21.2939999971965,19.2108801919503,3.43329010980363));
#131339=CARTESIAN_POINT('Ctrl Pts',(-21.2939999971965,19.2108801919503,
3.43329010980363));
#131340=CARTESIAN_POINT('Ctrl Pts',(-21.294003905102,19.2943824116244,3.43746913841141));
#131341=CARTESIAN_POINT('Ctrl Pts',(-21.2899179933662,19.3780422026729,
3.44164816701919));
#131342=CARTESIAN_POINT('Ctrl Pts',(-21.2817219740999,19.4614251239161,
3.44582719562696));
#131343=CARTESIAN_POINT('Ctrl Pts',(-21.2735376207105,19.5446893613373,
3.45000027597723));
#131344=CARTESIAN_POINT('Ctrl Pts',(-21.2612548239782,19.6276770564323,
3.45417335632749));
#131345=CARTESIAN_POINT('Ctrl Pts',(-21.2449053023278,19.7099534675119,
3.45834643667776));
#131346=CARTESIAN_POINT('Ctrl Pts',(-21.228391285294,19.7930576758855,3.46256150311585));
#131347=CARTESIAN_POINT('Ctrl Pts',(-21.2077282378307,19.875435728573,3.46677656955395));
#131348=CARTESIAN_POINT('Ctrl Pts',(-21.1830026840864,19.9566445891559,
3.47099163599204));
#131349=CARTESIAN_POINT('Ctrl Pts',(-21.1585674190593,20.0369000225192,
3.47515721572332));
#131350=CARTESIAN_POINT('Ctrl Pts',(-21.1301646741428,20.1160131199896,
3.47932279545459));
#131351=CARTESIAN_POINT('Ctrl Pts',(-21.0979289771719,20.1935679573886,
3.48348837518587));
#131352=CARTESIAN_POINT('Ctrl Pts',(-21.0657039544922,20.2710971138504,
3.48765257555778));
#131353=CARTESIAN_POINT('Ctrl Pts',(-21.0296486772609,20.347068609211,3.49181677592968));
#131354=CARTESIAN_POINT('Ctrl Pts',(-20.9899463178963,20.4210852080619,
3.49598097630159));
#131355=CARTESIAN_POINT('Ctrl Pts',(-20.9502451090693,20.4950996619801,
3.50014505599882));
#131356=CARTESIAN_POINT('Ctrl Pts',(-20.9068972472216,20.5671589258642,
3.50430913569605));
#131357=CARTESIAN_POINT('Ctrl Pts',(-20.8601318431733,20.6368903833901,
3.50847321539329));
#131358=CARTESIAN_POINT('Ctrl Pts',(-20.8123689128483,20.7081092430375,
3.51272611670985));
#131359=CARTESIAN_POINT('Ctrl Pts',(-20.7610412266545,20.7768994173757,
3.51697901802641));
#131360=CARTESIAN_POINT('Ctrl Pts',(-20.7064383509255,20.8428967344162,
3.52123191934297));
#131361=CARTESIAN_POINT('Ctrl Pts',(-20.6528987388227,20.9076089076671,
3.52540200532764));
#131362=CARTESIAN_POINT('Ctrl Pts',(-20.5962107113947,20.969635714652,3.5295720913123));
#131363=CARTESIAN_POINT('Ctrl Pts',(-20.5366855500212,21.0286701592271,
3.53374217729697));
#131364=CARTESIAN_POINT('Ctrl Pts',(-20.4753871892413,21.0894631852098,
3.53803648627948));
#131365=CARTESIAN_POINT('Ctrl Pts',(-20.411080380652,21.1470823903906,3.54233079526199));
#131366=CARTESIAN_POINT('Ctrl Pts',(-20.3441412203941,21.2012374859267,
3.54662510424449));
#131367=CARTESIAN_POINT('Ctrl Pts',(-20.2772020601362,21.2553925814628,
3.550919413227));
#131368=CARTESIAN_POINT('Ctrl Pts',(-20.2076310154016,21.306083314333,3.55521372220951));
#131369=CARTESIAN_POINT('Ctrl Pts',(-20.1358342086543,21.353069291934,3.55950803119202));
#131370=CARTESIAN_POINT('Ctrl Pts',(-20.0658710578792,21.3988552702266,
3.56369266558496));
#131371=CARTESIAN_POINT('Ctrl Pts',(-19.9935321931099,21.4412951999105,
3.56787729997789));
#131372=CARTESIAN_POINT('Ctrl Pts',(-19.9191711337672,21.4801340603157,
3.57206193437083));
#131373=CARTESIAN_POINT('Ctrl Pts',(-19.8449159181885,21.5189176384104,
3.57624061245465));
#131374=CARTESIAN_POINT('Ctrl Pts',(-19.7686446296092,21.5541101172785,
3.58041929053848));
#131375=CARTESIAN_POINT('Ctrl Pts',(-19.690739462204,21.5854998634368,3.58459796862231));
#131376=CARTESIAN_POINT('Ctrl Pts',(-19.6114379006597,21.6174522482367,
3.58885154650778));
#131377=CARTESIAN_POINT('Ctrl Pts',(-19.5304437130248,21.645463967428,3.59310512439324));
#131378=CARTESIAN_POINT('Ctrl Pts',(-19.4481859912097,21.6693609112496,
3.5973587022787));
#131379=CARTESIAN_POINT('Ctrl Pts',(-19.3675229958474,21.6927945661833,
3.60152981625654));
#131380=CARTESIAN_POINT('Ctrl Pts',(-19.2856454833722,21.7122714336375,
3.60570093023438));
#131381=CARTESIAN_POINT('Ctrl Pts',(-19.2029762398825,21.7276766352525,
3.60987204421222));
#131382=CARTESIAN_POINT('Ctrl Pts',(-19.1203347368559,21.7430766675032,
3.61404175853247));
#131383=CARTESIAN_POINT('Ctrl Pts',(-19.0369024823169,21.754407663177,3.61821147285273));
#131384=CARTESIAN_POINT('Ctrl Pts',(-18.9531132034119,21.7616056935737,
3.62238118717299));
#131385=CARTESIAN_POINT('Ctrl Pts',(-18.8693269060889,21.7688034678336,
3.62655075311692));
#131386=CARTESIAN_POINT('Ctrl Pts',(-18.7851840680774,21.7718685307012,
3.63072031906085));
#131387=CARTESIAN_POINT('Ctrl Pts',(-18.701122931338,21.7707888776921,3.63488988500478));
#131388=CARTESIAN_POINT('Ctrl Pts',(-18.6141063087263,21.769671265415,3.63920604774384));
#131389=CARTESIAN_POINT('Ctrl Pts',(-18.5271777668964,21.764112064791,3.64352221048289));
#131390=CARTESIAN_POINT('Ctrl Pts',(-18.4408207068909,21.7541566806023,
3.64783837322195));
#131391=CARTESIAN_POINT('Ctrl Pts',(-18.3572767190368,21.744525592007,3.65201393741352));
#131392=CARTESIAN_POINT('Ctrl Pts',(-18.2742680097319,21.7307804563761,
3.65618950160509));
#131393=CARTESIAN_POINT('Ctrl Pts',(-18.1922227301013,21.7130146661882,
3.66036506579666));
#131394=CARTESIAN_POINT('Ctrl Pts',(-18.1060335384334,21.6943515681706,
3.66475152780946));
#131395=CARTESIAN_POINT('Ctrl Pts',(-18.0209082233735,21.6712511277376,
3.66913798982226));
#131396=CARTESIAN_POINT('Ctrl Pts',(-17.937323903919,21.6438804323133,3.67352445183506));
#131397=CARTESIAN_POINT('Ctrl Pts',(-17.8537395844645,21.616509736889,3.67791091384786));
#131398=CARTESIAN_POINT('Ctrl Pts',(-17.7716967745983,21.584869066222,3.68229737586066));
#131399=CARTESIAN_POINT('Ctrl Pts',(-17.6916449845522,21.5491822045706,
3.68668383787346));
#131400=CARTESIAN_POINT('Ctrl Pts',(-17.6152764960367,21.5151373483269,
3.69086847226646));
#131401=CARTESIAN_POINT('Ctrl Pts',(-17.5404355759513,21.4772837399297,
3.69505310665946));
#131402=CARTESIAN_POINT('Ctrl Pts',(-17.4675280096793,21.4357805954145,
3.69923774105247));
#131403=CARTESIAN_POINT('Ctrl Pts',(-17.3947242183036,21.3943365254885,
3.70341641913637));
#131404=CARTESIAN_POINT('Ctrl Pts',(-17.3238487109965,21.3492534633187,
3.70759509722027));
#131405=CARTESIAN_POINT('Ctrl Pts',(-17.2552863124834,21.3007382205317,
3.71177377530417));
#131406=CARTESIAN_POINT('Ctrl Pts',(-17.185494982251,21.2513533768844,3.71602735318961));
#131407=CARTESIAN_POINT('Ctrl Pts',(-17.1181009417718,21.1984122950055,
3.72028093107506));
#131408=CARTESIAN_POINT('Ctrl Pts',(-17.0534828491143,21.142181530975,3.72453450896051));
#131409=CARTESIAN_POINT('Ctrl Pts',(-16.9901175042757,21.0870409100313,
3.72870562293841));
#131410=CARTESIAN_POINT('Ctrl Pts',(-16.9294217964541,21.0287373383807,
3.73287673691632));
#131411=CARTESIAN_POINT('Ctrl Pts',(-16.8717211662666,20.9675641307475,
3.73704785089422));
#131412=CARTESIAN_POINT('Ctrl Pts',(-16.8140398980829,20.9064114503749,
3.74121756521455));
#131413=CARTESIAN_POINT('Ctrl Pts',(-16.7593520269257,20.8423913807957,
3.74538727953487));
#131414=CARTESIAN_POINT('Ctrl Pts',(-16.7079460749928,20.7758340145085,
3.74955699385519));
#131415=CARTESIAN_POINT('Ctrl Pts',(-16.6565419523043,20.709279016618,3.75372655979918));
#131416=CARTESIAN_POINT('Ctrl Pts',(-16.6084197971687,20.6401872661385,
3.75789612574317));
#131417=CARTESIAN_POINT('Ctrl Pts',(-16.563826915519,20.5689207574061,3.76206569168716));
#131418=CARTESIAN_POINT('Ctrl Pts',(-16.5176662031606,20.4951486061414,
3.76638185442614));
#131419=CARTESIAN_POINT('Ctrl Pts',(-16.4752878401618,20.4190463693443,
3.77069801716511));
#131420=CARTESIAN_POINT('Ctrl Pts',(-16.4369153041021,20.3410450875393,
3.77501417990409));
#131421=CARTESIAN_POINT('Ctrl Pts',(-16.3997927493695,20.2655846892869,
3.77918974409572));
#131422=CARTESIAN_POINT('Ctrl Pts',(-16.3664191932582,20.1883475199533,
3.78336530828734));
#131423=CARTESIAN_POINT('Ctrl Pts',(-16.3369478575569,20.1097441384558,
3.78754087247896));
#131424=CARTESIAN_POINT('Ctrl Pts',(-16.3059879947494,20.0271706870175,
3.79192733449162));
#131425=CARTESIAN_POINT('Ctrl Pts',(-16.2793350909183,19.9430899381559,
3.79631379650427));
#131426=CARTESIAN_POINT('Ctrl Pts',(-16.257106907446,19.8579935146957,3.80070025851693));
#131427=CARTESIAN_POINT('Ctrl Pts',(-16.2348787239737,19.7728970912354,
3.80508672052958));
#131428=CARTESIAN_POINT('Ctrl Pts',(-16.2170753038451,19.6867855767773,
3.80947318254224));
#131429=CARTESIAN_POINT('Ctrl Pts',(-16.2037517912764,19.6001580684646,
3.81385964455489));
#131430=CARTESIAN_POINT('Ctrl Pts',(-16.1910413132713,19.5175164202231,
3.81804427894799));
#131431=CARTESIAN_POINT('Ctrl Pts',(-16.182360236898,19.4340976099864,3.8222289133411));
#131432=CARTESIAN_POINT('Ctrl Pts',(-16.1777943305988,19.3503290196653,
3.8264135477342));
#131433=CARTESIAN_POINT('Ctrl Pts',(-16.1732349233019,19.2666796635639,
3.83059222581821));
#131434=CARTESIAN_POINT('Ctrl Pts',(-16.1727790761929,19.182681971724,3.83477090390221));
#131435=CARTESIAN_POINT('Ctrl Pts',(-16.1764611917473,19.0987714640509,
3.83894958198622));
#131436=CARTESIAN_POINT('Ctrl Pts',(-16.1802093065767,19.0133569208348,
3.84320315987164));
#131437=CARTESIAN_POINT('Ctrl Pts',(-16.1882452624471,18.9280331946165,
3.84745673775706));
#131438=CARTESIAN_POINT('Ctrl Pts',(-16.2005498883094,18.8432629586582,
3.85171031564248));
#131439=CARTESIAN_POINT('Ctrl Pts',(-16.2126159649891,18.7601361591379,
3.85588142962049));
#131440=CARTESIAN_POINT('Ctrl Pts',(-16.2287866065493,18.6775420566423,
3.86005254359851));
#131441=CARTESIAN_POINT('Ctrl Pts',(-16.2489913365584,18.5959130609253,
3.86422365757652));
#131442=CARTESIAN_POINT('Ctrl Pts',(-16.2691892866753,18.5143114566062,
3.86839337189696));
#131443=CARTESIAN_POINT('Ctrl Pts',(-16.2934185263772,18.433674762078,3.87256308621739));
#131444=CARTESIAN_POINT('Ctrl Pts',(-16.3215576717044,18.3544242516581,
3.87673280053782));
#131445=CARTESIAN_POINT('Ctrl Pts',(-16.34969581572,18.2751765613115,3.88090236648193));
#131446=CARTESIAN_POINT('Ctrl Pts',(-16.3817434340024,18.1973153902312,
3.88507193242603));
#131447=CARTESIAN_POINT('Ctrl Pts',(-16.4175300086125,18.1212446242384,
3.88924149837014));
#131448=CARTESIAN_POINT('Ctrl Pts',(-16.4545747950374,18.0424993039591,
3.89355766110898));
#131449=CARTESIAN_POINT('Ctrl Pts',(-16.4956261286211,17.9656731098163,
3.89787382384783));
#131450=CARTESIAN_POINT('Ctrl Pts',(-16.5404425366714,17.8911872651488,
3.90218998658668));
#131451=CARTESIAN_POINT('Ctrl Pts',(-16.5837990549447,17.8191277890345,
3.90636555077843));
#131452=CARTESIAN_POINT('Ctrl Pts',(-16.6306788183656,17.749258894982,3.91054111497017));
#131453=CARTESIAN_POINT('Ctrl Pts',(-16.6808195479051,17.6819316460226,
3.91471667916191));
#131454=CARTESIAN_POINT('Ctrl Pts',(-16.7334927664929,17.6112038577767,
3.91910314117431));
#131455=CARTESIAN_POINT('Ctrl Pts',(-16.7897646588842,17.5432816689316,
3.92348960318672));
#131456=CARTESIAN_POINT('Ctrl Pts',(-16.8492855900873,17.4785302042842,
3.92787606519912));
#131457=CARTESIAN_POINT('Ctrl Pts',(-16.9088065212905,17.4137787396368,
3.93226252721152));
#131458=CARTESIAN_POINT('Ctrl Pts',(-16.9715760238565,17.3521983512227,
3.93664898922393));
#131459=CARTESIAN_POINT('Ctrl Pts',(-17.0372042845901,17.2941055584184,
3.94103545123633));
#131460=CARTESIAN_POINT('Ctrl Pts',(-17.0815714375447,17.2548326629447,
3.94400086322284));
#131461=CARTESIAN_POINT('Ctrl Pts',(-17.1273612095889,17.2170492008642,
3.94696627520936));
#131462=CARTESIAN_POINT('Ctrl Pts',(-17.174464231106,17.180864983421,3.94993168719587));
#131463=CARTESIAN_POINT('Ctrl Pts',(-17.174464231106,17.180864983421,3.1498113662728));
#131464=CARTESIAN_POINT('Ctrl Pts',(-17.2410961502261,17.1296788010395,
3.15398941925709));
#131465=CARTESIAN_POINT('Ctrl Pts',(-17.3101818955148,17.0818293110454,
3.15816747224137));
#131466=CARTESIAN_POINT('Ctrl Pts',(-17.3813458444593,17.0375403763818,
3.16234552522566));
#131467=CARTESIAN_POINT('Ctrl Pts',(-17.4526226812698,16.9931811858739,
3.16653020588439));
#131468=CARTESIAN_POINT('Ctrl Pts',(-17.5259838976535,16.95239404136,3.17071488654311));
#131469=CARTESIAN_POINT('Ctrl Pts',(-17.6010304532445,16.9153562980888,
3.17489956720183));
#131470=CARTESIAN_POINT('Ctrl Pts',(-17.6194485640172,16.906266403783,3.17592658185046));
#131471=CARTESIAN_POINT('Ctrl Pts',(-17.6379681017651,16.8974021130445,
3.17695359649909));
#131472=CARTESIAN_POINT('Ctrl Pts',(-17.6565830150582,16.8887655931067,
3.17798061114772));
#131473=CARTESIAN_POINT('Ctrl Pts',(-17.7324306249075,16.8535755610943,
3.18216524554016));
#131474=CARTESIAN_POINT('Ctrl Pts',(-17.8101452346758,16.8220398921685,
3.18634987993261));
#131475=CARTESIAN_POINT('Ctrl Pts',(-17.8893401694872,16.7943598176977,
3.19053451432505));
#131476=CARTESIAN_POINT('Ctrl Pts',(-17.9684223801113,16.7667191423868,
3.19471319240839));
#131477=CARTESIAN_POINT('Ctrl Pts',(-18.0489802999388,16.7429233111999,
3.19889187049173));
#131478=CARTESIAN_POINT('Ctrl Pts',(-18.1306051532976,16.7231264785016,
3.20307054857507));
#131479=CARTESIAN_POINT('Ctrl Pts',(-18.2136930735051,16.7029748018013,
3.20732412646065));
#131480=CARTESIAN_POINT('Ctrl Pts',(-18.297886115673,16.6869671007255,3.21157770434624));
#131481=CARTESIAN_POINT('Ctrl Pts',(-18.3827345240938,16.6752136199127,
3.21583128223183));
#131482=CARTESIAN_POINT('Ctrl Pts',(-18.4659379805342,16.6636880032625,
3.22000239620917));
#131483=CARTESIAN_POINT('Ctrl Pts',(-18.5497711422169,16.6562531921902,
3.22417351018651));
#131484=CARTESIAN_POINT('Ctrl Pts',(-18.6337990563683,16.6529617338876,
3.22834462416386));
#131485=CARTESIAN_POINT('Ctrl Pts',(-18.7177987741417,16.6496713800656,
3.23251433848362));
#131486=CARTESIAN_POINT('Ctrl Pts',(-18.8019926552977,16.6505216357632,
3.23668405280339));
#131487=CARTESIAN_POINT('Ctrl Pts',(-18.885942287003,16.6555130519957,3.24085376712315));
#131488=CARTESIAN_POINT('Ctrl Pts',(-18.9698889314202,16.6605042906123,
3.24502333306659));
#131489=CARTESIAN_POINT('Ctrl Pts',(-19.0535908844962,16.669636368619,3.24919289901003));
#131490=CARTESIAN_POINT('Ctrl Pts',(-19.1366127729526,16.6828578056099,
3.25336246495347));
#131491=CARTESIAN_POINT('Ctrl Pts',(-19.2225536086153,16.6965440920193,
3.25767862769311));
#131492=CARTESIAN_POINT('Ctrl Pts',(-19.3077651468771,16.7146125685867,
3.26199479043275));
#131493=CARTESIAN_POINT('Ctrl Pts',(-19.3917756297612,16.7369484199208,
3.26631095317239));
#131494=CARTESIAN_POINT('Ctrl Pts',(-19.4730494799765,16.7585566832404,
3.27048651736348));
#131495=CARTESIAN_POINT('Ctrl Pts',(-19.5531988875823,16.7841583830433,
3.27466208155456));
#131496=CARTESIAN_POINT('Ctrl Pts',(-19.6318137018712,16.8135992081564,
3.27883764574565));
#131497=CARTESIAN_POINT('Ctrl Pts',(-19.7143991635786,16.8445270193712,
3.28322410775957));
#131498=CARTESIAN_POINT('Ctrl Pts',(-19.7952903977548,16.8796917438777,
3.28761056977348));
#131499=CARTESIAN_POINT('Ctrl Pts',(-19.8740394547192,16.9188590702831,
3.2919970317874));
#131500=CARTESIAN_POINT('Ctrl Pts',(-19.9527885116835,16.9580263966884,
3.29638349380132));
#131501=CARTESIAN_POINT('Ctrl Pts',(-20.0293949232977,17.0011959738741,
3.30076995581524));
#131502=CARTESIAN_POINT('Ctrl Pts',(-20.1034462555219,17.0480813808104,
3.30515641782916));
#131503=CARTESIAN_POINT('Ctrl Pts',(-20.1740903761505,17.092809520654,3.30934105222176));
#131504=CARTESIAN_POINT('Ctrl Pts',(-20.2426723273843,17.1410855493988,
3.31352568661436));
#131505=CARTESIAN_POINT('Ctrl Pts',(-20.3088136057117,17.19269325739,3.31771032100697));
#131506=CARTESIAN_POINT('Ctrl Pts',(-20.374860740116,17.2442275081965,3.32188899909046));
#131507=CARTESIAN_POINT('Ctrl Pts',(-20.4384737424745,17.2990837381083,
3.32606767717394));
#131508=CARTESIAN_POINT('Ctrl Pts',(-20.4993017308437,17.3570016723092,
3.33024635525743));
#131509=CARTESIAN_POINT('Ctrl Pts',(-20.5612200171964,17.4159577438638,
3.33449993314298));
#131510=CARTESIAN_POINT('Ctrl Pts',(-20.6202520574043,17.4780861035065,
3.33875351102853));
#131511=CARTESIAN_POINT('Ctrl Pts',(-20.6760617089389,17.5430682511945,
3.34300708891408));
#131512=CARTESIAN_POINT('Ctrl Pts',(-20.7307893814672,17.6067905931385,
3.34717820289156));
#131513=CARTESIAN_POINT('Ctrl Pts',(-20.7824181813928,17.6732566930095,
3.35134931686903));
#131514=CARTESIAN_POINT('Ctrl Pts',(-20.8306684931563,17.742129267156,3.35552043084651));
#131515=CARTESIAN_POINT('Ctrl Pts',(-20.8789026140616,17.810978730445,3.3596901451664));
#131516=CARTESIAN_POINT('Ctrl Pts',(-20.923760234583,17.8822326878121,3.36385985948629));
#131517=CARTESIAN_POINT('Ctrl Pts',(-20.9650035868519,17.955522801699,3.36802957380618));
#131518=CARTESIAN_POINT('Ctrl Pts',(-21.0062454715054,18.028810307609,3.37219913974974));
#131519=CARTESIAN_POINT('Ctrl Pts',(-21.0438731187515,18.1041334246492,
3.37636870569329));
#131520=CARTESIAN_POINT('Ctrl Pts',(-21.0776941561666,18.1810982074244,
3.38053827163685));
#131521=CARTESIAN_POINT('Ctrl Pts',(-21.1127042995431,18.2607689770352,
3.38485443437633));
#131522=CARTESIAN_POINT('Ctrl Pts',(-21.1436349596428,18.3421985193634,
3.3891705971158));
#131523=CARTESIAN_POINT('Ctrl Pts',(-21.1703273243944,18.4249280132143,
3.39348675985528));
#131524=CARTESIAN_POINT('Ctrl Pts',(-21.1961501881654,18.5049626024847,
3.39766232404647));
#131525=CARTESIAN_POINT('Ctrl Pts',(-21.2180065643708,18.5862132848946,
3.40183788823765));
#131526=CARTESIAN_POINT('Ctrl Pts',(-21.2358041974883,18.6682516628954,
3.40601345242883));
#131527=CARTESIAN_POINT('Ctrl Pts',(-21.2545007467516,18.7544336043729,
3.41039991444246));
#131528=CARTESIAN_POINT('Ctrl Pts',(-21.2687176692139,18.8414843294195,
3.41478637645609));
#131529=CARTESIAN_POINT('Ctrl Pts',(-21.2784095170101,18.9289003549305,
3.41917283846971));
#131530=CARTESIAN_POINT('Ctrl Pts',(-21.2881013648063,19.0163163804415,
3.42355930048334));
#131531=CARTESIAN_POINT('Ctrl Pts',(-21.293268179777,19.1040971227328,3.42794576249697));
#131532=CARTESIAN_POINT('Ctrl Pts',(-21.2939275539577,19.1917407557754,
3.43233222451059));
#131533=CARTESIAN_POINT('Ctrl Pts',(-21.2939755504833,19.1981204260763,
3.43265151959756));
#131534=CARTESIAN_POINT('Ctrl Pts',(-21.2939996986147,19.2045002760229,
3.43297081468453));
#131535=CARTESIAN_POINT('Ctrl Pts',(-21.2939999971965,19.2108801913083,
3.4332901097715));
#131536=CARTESIAN_POINT('',(-21.2936055426903,19.2106176052578,3.36670986511441));
#131537=CARTESIAN_POINT('Ctrl Pts',(-17.1746506278756,17.1811162280172,
3.08342410660674));
#131538=CARTESIAN_POINT('Ctrl Pts',(-17.6886694547963,16.794397148351,3.11541446008311));
#131539=CARTESIAN_POINT('Ctrl Pts',(-19.2309397104083,16.3326325381546,
3.18979674911996));
#131540=CARTESIAN_POINT('Ctrl Pts',(-21.0089154299348,17.5465283377359,
3.28422525530949));
#131541=CARTESIAN_POINT('Ctrl Pts',(-21.290373212379,18.8060182046973,3.34666340802265));
#131542=CARTESIAN_POINT('Ctrl Pts',(-21.2898371856445,19.2106133247715,
3.36670962517532));
#131543=CARTESIAN_POINT('Ctrl Pts',(-21.2939999715072,19.2106180532905,
3.36670989022851));
#131544=CARTESIAN_POINT('Ctrl Pts',(-21.2940130064034,19.2979845189442,
3.37103154303559));
#131545=CARTESIAN_POINT('Ctrl Pts',(-21.2895493128086,19.3852864628676,
3.37535319584268));
#131546=CARTESIAN_POINT('Ctrl Pts',(-21.2806546261691,19.4720559614555,
3.37967484864976));
#131547=CARTESIAN_POINT('Ctrl Pts',(-21.2713805337796,19.5625266412119,
3.38418084296218));
#131548=CARTESIAN_POINT('Ctrl Pts',(-21.2572890869444,19.6524179424097,
3.38868683727459));
#131549=CARTESIAN_POINT('Ctrl Pts',(-21.2384911684206,19.7412112666692,
3.393192831587));
#131550=CARTESIAN_POINT('Ctrl Pts',(-21.2204017935413,19.8266577339088,
3.3975289829656));
#131551=CARTESIAN_POINT('Ctrl Pts',(-21.1979545494935,19.911087135192,3.40186513434419));
#131552=CARTESIAN_POINT('Ctrl Pts',(-21.1712990035409,19.9940540002698,
3.40620128572279));
#131553=CARTESIAN_POINT('Ctrl Pts',(-21.1446099328528,20.0771252129461,
3.41054289068797));
#131554=CARTESIAN_POINT('Ctrl Pts',(-21.1137021554183,20.1587298407179,
3.41488449565315));
#131555=CARTESIAN_POINT('Ctrl Pts',(-21.0787731611217,20.2384428562617,
3.41922610061834));
#131556=CARTESIAN_POINT('Ctrl Pts',(-21.0437703953367,20.3183242290092,
3.42357687523375));
#131557=CARTESIAN_POINT('Ctrl Pts',(-21.0047296348366,20.3963056454717,
3.42792764984916));
#131558=CARTESIAN_POINT('Ctrl Pts',(-20.9618940508659,20.4719869539834,
3.43227842446457));
#131559=CARTESIAN_POINT('Ctrl Pts',(-20.9570751477604,20.4805009243513,
3.43276787644263));
#131560=CARTESIAN_POINT('Ctrl Pts',(-20.9522082623986,20.4889858169837,
3.43325732842068));
#131561=CARTESIAN_POINT('Ctrl Pts',(-20.9472937739975,20.4974410868688,
3.43374678039873));
#131562=CARTESIAN_POINT('Ctrl Pts',(-20.9052767057113,20.5697305345463,
3.43793141479118));
#131563=CARTESIAN_POINT('Ctrl Pts',(-20.8596361007269,20.6400938357955,
3.44211604918362));
#131564=CARTESIAN_POINT('Ctrl Pts',(-20.8105736599315,20.7081445604478,
3.44630068357607));
#131565=CARTESIAN_POINT('Ctrl Pts',(-20.7615810534479,20.7760984233165,
3.45047936165941));
#131566=CARTESIAN_POINT('Ctrl Pts',(-20.7091765523538,20.8417458779045,
3.45465803974274));
#131567=CARTESIAN_POINT('Ctrl Pts',(-20.6536069384425,20.9047264247462,
3.45883671782608));
#131568=CARTESIAN_POINT('Ctrl Pts',(-20.5970412791288,20.9688358526383,
3.46309029571167));
#131569=CARTESIAN_POINT('Ctrl Pts',(-20.5371961639062,21.0301814068962,
3.46734387359725));
#131570=CARTESIAN_POINT('Ctrl Pts',(-20.4743771168498,21.0884151089052,
3.47159745148284));
#131571=CARTESIAN_POINT('Ctrl Pts',(-20.412775939613,21.1455198369568,3.47576856546018));
#131572=CARTESIAN_POINT('Ctrl Pts',(-20.3483154653815,21.1996319675306,
3.47993967943753));
#131573=CARTESIAN_POINT('Ctrl Pts',(-20.2813221318913,21.250459296029,3.48411079341487));
#131574=CARTESIAN_POINT('Ctrl Pts',(-20.2143512786613,21.3012695689265,
3.48828050773464));
#131575=CARTESIAN_POINT('Ctrl Pts',(-20.1448496203246,21.3487969510057,
3.4924502220544));
#131576=CARTESIAN_POINT('Ctrl Pts',(-20.0731762130974,21.3927898776633,
3.49661993637416));
#131577=CARTESIAN_POINT('Ctrl Pts',(-20.0015053563176,21.4367812388638,
3.50078950231759));
#131578=CARTESIAN_POINT('Ctrl Pts',(-19.9276632968144,21.4772381547836,
3.50495906826103));
#131579=CARTESIAN_POINT('Ctrl Pts',(-19.8520364016656,21.5139534525367,
3.50912863420446));
#131580=CARTESIAN_POINT('Ctrl Pts',(-19.7737505581546,21.5519596148775,
3.5134447969441));
#131581=CARTESIAN_POINT('Ctrl Pts',(-19.6935525085944,21.585955922694,3.51776095968374));
#131582=CARTESIAN_POINT('Ctrl Pts',(-19.6118947218442,21.6157662791544,
3.52207712242338));
#131583=CARTESIAN_POINT('Ctrl Pts',(-19.5328969289329,21.6446055663797,
3.52625268661447));
#131584=CARTESIAN_POINT('Ctrl Pts',(-19.4525335041393,21.6695273345314,
3.53042825080555));
#131585=CARTESIAN_POINT('Ctrl Pts',(-19.3712290384541,21.690423149152,3.53460381499663));
#131586=CARTESIAN_POINT('Ctrl Pts',(-19.2858180774511,21.712374361704,3.53899027701055));
#131587=CARTESIAN_POINT('Ctrl Pts',(-19.1993690855429,21.7298821146793,
3.54337673902448));
#131588=CARTESIAN_POINT('Ctrl Pts',(-19.1123834602667,21.7428819002861,
3.5477632010384));
#131589=CARTESIAN_POINT('Ctrl Pts',(-19.0253978349904,21.755881685893,3.55214966305232));
#131590=CARTESIAN_POINT('Ctrl Pts',(-18.9378761611969,21.7643735238079,
3.55653612506624));
#131591=CARTESIAN_POINT('Ctrl Pts',(-18.8503205710795,21.7683559636358,
3.56092258708016));
#131592=CARTESIAN_POINT('Ctrl Pts',(-18.7667935434871,21.7721551655022,
3.56510722147276));
#131593=CARTESIAN_POINT('Ctrl Pts',(-18.6829247485325,21.771864959913,3.56929185586537));
#131594=CARTESIAN_POINT('Ctrl Pts',(-18.5991482896985,21.7674457780733,
3.57347649025797));
#131595=CARTESIAN_POINT('Ctrl Pts',(-18.5154910762845,21.7630328863919,
3.57765516834146));
#131596=CARTESIAN_POINT('Ctrl Pts',(-18.4319263933964,21.7545027162291,
3.58183384642494));
#131597=CARTESIAN_POINT('Ctrl Pts',(-18.3488909423388,21.7418676404955,
3.58601252450843));
#131598=CARTESIAN_POINT('Ctrl Pts',(-18.264367140486,21.7290060901083,3.59026610239398));
#131599=CARTESIAN_POINT('Ctrl Pts',(-18.1803922116833,21.7118910039099,
3.59451968027953));
#131600=CARTESIAN_POINT('Ctrl Pts',(-18.0974241252639,21.6905909250729,
3.59877325816508));
#131601=CARTESIAN_POINT('Ctrl Pts',(-18.0160645371101,21.6697037898308,
3.60294437214255));
#131602=CARTESIAN_POINT('Ctrl Pts',(-17.9356735666136,21.6447926020537,
3.60711548612003));
#131603=CARTESIAN_POINT('Ctrl Pts',(-17.8566736061543,21.6159736794114,
3.61128660009751));
#131604=CARTESIAN_POINT('Ctrl Pts',(-17.7777001548947,21.5871644272369,
3.6154563144174));
#131605=CARTESIAN_POINT('Ctrl Pts',(-17.7001172184808,21.5544502019411,
3.61962602873729));
#131606=CARTESIAN_POINT('Ctrl Pts',(-17.6243306732528,21.5179967458313,
3.62379574305719));
#131607=CARTESIAN_POINT('Ctrl Pts',(-17.5485468248354,21.481544586892,3.62796530900075));
#131608=CARTESIAN_POINT('Ctrl Pts',(-17.4745596547068,21.4413536618678,
3.63213487494431));
#131609=CARTESIAN_POINT('Ctrl Pts',(-17.4027524956497,21.3976367055734,
3.63630444088787));
#131610=CARTESIAN_POINT('Ctrl Pts',(-17.3284206854458,21.3523827150154,
3.64062060362735));
#131611=CARTESIAN_POINT('Ctrl Pts',(-17.2564254874566,21.3033504035823,
3.64493676636682));
#131612=CARTESIAN_POINT('Ctrl Pts',(-17.1871598840616,21.2508249081045,
3.6492529291063));
#131613=CARTESIAN_POINT('Ctrl Pts',(-17.1201506004284,21.2000104251299,
3.65342849329749));
#131614=CARTESIAN_POINT('Ctrl Pts',(-17.0556961397385,21.1459271830849,
3.65760405748867));
#131615=CARTESIAN_POINT('Ctrl Pts',(-16.9941175012612,21.0888735022845,
3.66177962167986));
#131616=CARTESIAN_POINT('Ctrl Pts',(-16.92942867212,21.0289381756772,3.66616608369348));
#131617=CARTESIAN_POINT('Ctrl Pts',(-16.8679142228486,20.965724868959,3.6705525457071));
#131618=CARTESIAN_POINT('Ctrl Pts',(-16.8098997912682,20.899620261266,3.67493900772073));
#131619=CARTESIAN_POINT('Ctrl Pts',(-16.7518853596878,20.8335156535731,
3.67932546973435));
#131620=CARTESIAN_POINT('Ctrl Pts',(-16.6973712458222,20.7645202473232,
3.68371193174797));
#131621=CARTESIAN_POINT('Ctrl Pts',(-16.6466304638568,20.6930554711553,
3.68809839376159));
#131622=CARTESIAN_POINT('Ctrl Pts',(-16.5982243404927,20.6248788952851,
3.69228302815505));
#131623=CARTESIAN_POINT('Ctrl Pts',(-16.553071769447,20.5542014284548,3.69646766254851));
#131624=CARTESIAN_POINT('Ctrl Pts',(-16.511440993796,20.4813666651568,3.70065229694197));
#131625=CARTESIAN_POINT('Ctrl Pts',(-16.4698694744012,20.4086355731289,
3.70483097502634));
#131626=CARTESIAN_POINT('Ctrl Pts',(-16.4318100196565,20.3337536798782,
3.70900965311071));
#131627=CARTESIAN_POINT('Ctrl Pts',(-16.3974886040354,20.2570948793143,
3.71318833119508));
#131628=CARTESIAN_POINT('Ctrl Pts',(-16.3625520017101,20.1790620248538,
3.71744190908041));
#131629=CARTESIAN_POINT('Ctrl Pts',(-16.3314890444372,20.0991883275084,
3.72169548696574));
#131630=CARTESIAN_POINT('Ctrl Pts',(-16.3044899883693,20.0178959681312,
3.72594906485107));
#131631=CARTESIAN_POINT('Ctrl Pts',(-16.2780143616844,19.9381796197593,
3.73012017882945));
#131632=CARTESIAN_POINT('Ctrl Pts',(-16.2554466207296,19.8570995822354,
3.73429129280783));
#131633=CARTESIAN_POINT('Ctrl Pts',(-16.2369175937362,19.7750739812542,
3.73846240678621));
#131634=CARTESIAN_POINT('Ctrl Pts',(-16.2183947843368,19.6930759047555,
3.74263212110702));
#131635=CARTESIAN_POINT('Ctrl Pts',(-16.2039080986716,19.6101333433014,
3.74680183542783));
#131636=CARTESIAN_POINT('Ctrl Pts',(-16.1935378668542,19.5266772878306,
3.75097154974863));
#131637=CARTESIAN_POINT('Ctrl Pts',(-16.1831680040541,19.4432242020842,
3.75514111569312));
#131638=CARTESIAN_POINT('Ctrl Pts',(-16.1769143597415,19.3592581152781,
3.7593106816376));
#131639=CARTESIAN_POINT('Ctrl Pts',(-16.174805548368,19.2752164989395,3.76348024758209));
#131640=CARTESIAN_POINT('Ctrl Pts',(-16.1726225937887,19.1882200830664,
3.7677964103205));
#131641=CARTESIAN_POINT('Ctrl Pts',(-16.1748813730051,19.1011432548615,
3.77211257305891));
#131642=CARTESIAN_POINT('Ctrl Pts',(-16.1815548449752,19.0144707894728,
3.77642873579732));
#131643=CARTESIAN_POINT('Ctrl Pts',(-16.1880109292992,18.9306216705092,
3.78060429998944));
#131644=CARTESIAN_POINT('Ctrl Pts',(-16.1985983999138,18.8471514360442,
3.78477986418156));
#131645=CARTESIAN_POINT('Ctrl Pts',(-16.2132401674605,18.7644914707922,
3.78895542837368));
#131646=CARTESIAN_POINT('Ctrl Pts',(-16.2286214558734,18.6776565472293,
3.79334189038524));
#131647=CARTESIAN_POINT('Ctrl Pts',(-16.2484772384201,18.5917164663174,
3.7977283523968));
#131648=CARTESIAN_POINT('Ctrl Pts',(-16.272658640717,18.5071543400128,3.80211481440835));
#131649=CARTESIAN_POINT('Ctrl Pts',(-16.2968400430139,18.4225922137082,
3.80650127641991));
#131650=CARTESIAN_POINT('Ctrl Pts',(-16.3253468050044,18.3394085662324,
3.81088773843147));
#131651=CARTESIAN_POINT('Ctrl Pts',(-16.3579723492966,18.2580610706385,
3.81527420044303));
#131652=CARTESIAN_POINT('Ctrl Pts',(-16.3890953380446,18.1804599993008,
3.81945864581525));
#131653=CARTESIAN_POINT('Ctrl Pts',(-16.424081917038,18.1042408407701,3.82364309118746));
#131654=CARTESIAN_POINT('Ctrl Pts',(-16.4627883931758,18.0298150707755,
3.82782753655968));
#131655=CARTESIAN_POINT('Ctrl Pts',(-16.5014420742954,17.9554908163484,
3.83200627441491));
#131656=CARTESIAN_POINT('Ctrl Pts',(-16.5438053666935,17.8829554976016,
3.83618501227014));
#131657=CARTESIAN_POINT('Ctrl Pts',(-16.5896861940407,17.8126015226079,
3.84036375012537));
#131658=CARTESIAN_POINT('Ctrl Pts',(-16.635512417077,17.7423312782389,3.84453751472457));
#131659=CARTESIAN_POINT('Ctrl Pts',(-16.6848476027862,17.6742375999541,
3.84871127932376));
#131660=CARTESIAN_POINT('Ctrl Pts',(-16.7374540925027,17.6086877834655,
3.85288504392296));
#131661=CARTESIAN_POINT('Ctrl Pts',(-16.7900243343834,17.5431831332481,
3.8570559326425));
#131662=CARTESIAN_POINT('Ctrl Pts',(-16.8458611158911,17.4802192208169,
3.86122682136205));
#131663=CARTESIAN_POINT('Ctrl Pts',(-16.9046845018978,17.4201329450786,
3.86539771008159));
#131664=CARTESIAN_POINT('Ctrl Pts',(-16.9634896683862,17.3600652800165,
3.86956730694107));
#131665=CARTESIAN_POINT('Ctrl Pts',(-17.0252792822166,17.3028738113101,
3.87373690380055));
#131666=CARTESIAN_POINT('Ctrl Pts',(-17.0897351511635,17.2488600694954,
3.87790650066003));
#131667=CARTESIAN_POINT('Ctrl Pts',(-17.1174932740853,17.2255988815034,
3.87970215067687));
#131668=CARTESIAN_POINT('Ctrl Pts',(-17.1457454288767,17.2029265699414,
3.8814978006937));
#131669=CARTESIAN_POINT('Ctrl Pts',(-17.174464231106,17.180864983421,3.88329345071054));
#131670=CARTESIAN_POINT('Origin',(-18.734,19.211,-1.76670989022852));
#131671=CARTESIAN_POINT('',(-17.1762220704532,17.1831893817011,4.7499734657924));
#131672=CARTESIAN_POINT('',(-17.1735447493683,17.1796894255362,4.68319930527189));
#131673=CARTESIAN_POINT('',(-17.174464231106,17.180864983421,-1.76670989022852));
#131674=CARTESIAN_POINT('',(-21.2939990418858,19.2087851537695,4.23329008725203));
#131675=CARTESIAN_POINT('Ctrl Pts',(-21.2923873880696,19.2087870015046,
4.2332901097715));
#131676=CARTESIAN_POINT('Ctrl Pts',(-21.2874613882922,19.8078856368616,
4.26304769694121));
#131677=CARTESIAN_POINT('Ctrl Pts',(-20.7784814085672,21.2679844548948,
4.3351972196714));
#131678=CARTESIAN_POINT('Ctrl Pts',(-18.3440265327566,22.212868160657,4.44973867796206));
#131679=CARTESIAN_POINT('Ctrl Pts',(-15.9988186914362,20.5079483291182,
4.5769144846435));
#131680=CARTESIAN_POINT('Ctrl Pts',(-16.1279939788785,18.2299561235477,
4.67699274725361));
#131681=CARTESIAN_POINT('Ctrl Pts',(-16.9304194998099,17.3693100983237,
4.73467907430325));
#131682=CARTESIAN_POINT('Ctrl Pts',(-17.1762220704533,17.183189381701,4.74997346579241));
#131683=CARTESIAN_POINT('Ctrl Pts',(-17.174464231106,17.180864983421,3.94993168719587));
#131684=CARTESIAN_POINT('Ctrl Pts',(-17.2408642333853,17.1298569579628,
3.95411195751233));
#131685=CARTESIAN_POINT('Ctrl Pts',(-17.3098752464746,17.0820286544136,
3.95829222782878));
#131686=CARTESIAN_POINT('Ctrl Pts',(-17.3811592903901,17.0376564895484,
3.96247249814524));
#131687=CARTESIAN_POINT('Ctrl Pts',(-17.4523586048633,16.9933370662026,
3.9666477997204));
#131688=CARTESIAN_POINT('Ctrl Pts',(-17.5258251943333,16.9524658616689,
3.97082310129556));
#131689=CARTESIAN_POINT('Ctrl Pts',(-17.6011899553232,16.915277585883,3.97499840287073));
#131690=CARTESIAN_POINT('Ctrl Pts',(-17.6764915764994,16.8781204660482,
3.9791702064216));
#131691=CARTESIAN_POINT('Ctrl Pts',(-17.7536877979744,16.8446403465275,
3.98334200997247));
#131692=CARTESIAN_POINT('Ctrl Pts',(-17.832383755932,16.8150266803588,3.98751381352334));
#131693=CARTESIAN_POINT('Ctrl Pts',(-17.9110459750257,16.7854257102862,
3.99168382852096));
#131694=CARTESIAN_POINT('Ctrl Pts',(-17.9912062238471,16.7596880637534,
3.99585384351857));
#131695=CARTESIAN_POINT('Ctrl Pts',(-18.0724495705645,16.7379551097253,
4.00002385851619));
#131696=CARTESIAN_POINT('Ctrl Pts',(-18.1536824574235,16.7162249537556,
4.0041933366358));
#131697=CARTESIAN_POINT('Ctrl Pts',(-18.235997720657,16.6984985843148,4.0083628147554));
#131698=CARTESIAN_POINT('Ctrl Pts',(-18.3189664976901,16.6848671468111,
4.01253229287501));
#131699=CARTESIAN_POINT('Ctrl Pts',(-18.4019494810084,16.6712333752716,
4.01670248491132));
#131700=CARTESIAN_POINT('Ctrl Pts',(-18.4855857462034,16.6616960011917,
4.02087267694763));
#131701=CARTESIAN_POINT('Ctrl Pts',(-18.569438860629,16.6562946096646,4.02504286898394));
#131702=CARTESIAN_POINT('Ctrl Pts',(-18.6533844036521,16.6508872643569,
4.02921765768912));
#131703=CARTESIAN_POINT('Ctrl Pts',(-18.7375468131607,16.6496250298472,
4.0333924463943));
#131704=CARTESIAN_POINT('Ctrl Pts',(-18.8214877370601,16.6524953789637,
4.03756723509948));
#131705=CARTESIAN_POINT('Ctrl Pts',(-18.9054812334263,16.655367525789,4.04174463848807));
#131706=CARTESIAN_POINT('Ctrl Pts',(-18.9892525099869,16.6623773694637,
4.04592204187665));
#131707=CARTESIAN_POINT('Ctrl Pts',(-19.0723688153353,16.6734605333496,
4.05009944526523));
#131708=CARTESIAN_POINT('Ctrl Pts',(-19.1556216891913,16.6845619079962,
4.05428371255066));
#131709=CARTESIAN_POINT('Ctrl Pts',(-19.2382169920771,16.6997498783073,
4.0584679798361));
#131710=CARTESIAN_POINT('Ctrl Pts',(-19.3197330693514,16.7189091566582,
4.06265224712154));
#131711=CARTESIAN_POINT('Ctrl Pts',(-19.355832480369,16.7273938468827,4.06450525072028));
#131712=CARTESIAN_POINT('Ctrl Pts',(-19.391720451714,16.736656722528,4.06635825431902));
#131713=CARTESIAN_POINT('Ctrl Pts',(-19.4273615317729,16.7466847226344,
4.06821125791776));
#131714=CARTESIAN_POINT('Ctrl Pts',(-19.5078497129729,16.7693309356085,
4.0723958923108));
#131715=CARTESIAN_POINT('Ctrl Pts',(-19.5873770243864,16.7959667334644,
4.07658052670384));
#131716=CARTESIAN_POINT('Ctrl Pts',(-19.6655189252299,16.826493239276,4.08076516109689));
#131717=CARTESIAN_POINT('Ctrl Pts',(-19.7435496007498,16.8569762943851,
4.08494383918084));
#131718=CARTESIAN_POINT('Ctrl Pts',(-19.8201983578021,16.8913388913937,
4.08912251726478));
#131719=CARTESIAN_POINT('Ctrl Pts',(-19.8950545149197,16.9294320274459,
4.09330119534873));
#131720=CARTESIAN_POINT('Ctrl Pts',(-19.9712524148554,16.9682079555848,
4.09755477323417));
#131721=CARTESIAN_POINT('Ctrl Pts',(-20.0455923539259,17.0108493474662,
4.1018083511196));
#131722=CARTESIAN_POINT('Ctrl Pts',(-20.1176611149876,17.0571471919207,
4.10606192900504));
#131723=CARTESIAN_POINT('Ctrl Pts',(-20.1883326824854,17.1025474623176,
4.11023304298298));
#131724=CARTESIAN_POINT('Ctrl Pts',(-20.2568199436827,17.1514634154309,
4.11440415696093));
#131725=CARTESIAN_POINT('Ctrl Pts',(-20.3227584711506,17.2036518686717,
4.11857527093887));
#131726=CARTESIAN_POINT('Ctrl Pts',(-20.3886748723087,17.2558228095729,
4.12274498525923));
#131727=CARTESIAN_POINT('Ctrl Pts',(-20.4520438778608,17.3112637844568,
4.1269146995796));
#131728=CARTESIAN_POINT('Ctrl Pts',(-20.5125322737859,17.369689881877,4.13108441389996));
#131729=CARTESIAN_POINT('Ctrl Pts',(-20.5730185172744,17.4281139002461,
4.13525397984401));
#131730=CARTESIAN_POINT('Ctrl Pts',(-20.6306240246489,17.4895225097361,
4.13942354578805));
#131731=CARTESIAN_POINT('Ctrl Pts',(-20.685051752926,17.5535932733923,4.14359311173209));
#131732=CARTESIAN_POINT('Ctrl Pts',(-20.7413930929855,17.619916686059,4.14790927447102));
#131733=CARTESIAN_POINT('Ctrl Pts',(-20.7943286933424,17.6890925366907,
4.15222543720994));
#131734=CARTESIAN_POINT('Ctrl Pts',(-20.8435751066799,17.760726622572,4.15654159994887));
#131735=CARTESIAN_POINT('Ctrl Pts',(-20.8912173232827,17.8300272356402,
4.16071716414055));
#131736=CARTESIAN_POINT('Ctrl Pts',(-20.9354068051751,17.9016279637399,
4.16489272833223));
#131737=CARTESIAN_POINT('Ctrl Pts',(-20.9759325838399,17.9751447133596,
4.16906829252391));
#131738=CARTESIAN_POINT('Ctrl Pts',(-21.0185052232442,18.0523746192331,
4.17345475453645));
#131739=CARTESIAN_POINT('Ctrl Pts',(-21.0570340704739,18.1317186646461,
4.177841216549));
#131740=CARTESIAN_POINT('Ctrl Pts',(-21.091331525063,18.2127074171646,4.18222767856155));
#131741=CARTESIAN_POINT('Ctrl Pts',(-21.1256289796521,18.2936961696831,
4.1866141405741));
#131742=CARTESIAN_POINT('Ctrl Pts',(-21.1556949146933,18.3763290580523,
4.19100060258664));
#131743=CARTESIAN_POINT('Ctrl Pts',(-21.1814026084241,18.4601202011779,
4.19538706459919));
#131744=CARTESIAN_POINT('Ctrl Pts',(-21.211365847261,18.557781782967,4.20049964335899));
#131745=CARTESIAN_POINT('Ctrl Pts',(-21.2355013786602,18.6573099274653,
4.20561222211879));
#131746=CARTESIAN_POINT('Ctrl Pts',(-21.2536149670824,18.758075704279,4.21072480087859));
#131747=CARTESIAN_POINT('Ctrl Pts',(-21.271481685507,18.8574681448711,4.2157677003304));
#131748=CARTESIAN_POINT('Ctrl Pts',(-21.2834894543748,18.9580647258708,
4.22081059978222));
#131749=CARTESIAN_POINT('Ctrl Pts',(-21.289497836736,19.0592409592887,4.22585349923404));
#131750=CARTESIAN_POINT('Ctrl Pts',(-21.2924512874047,19.1089746473736,
4.2283323619067));
#131751=CARTESIAN_POINT('Ctrl Pts',(-21.293955837589,19.1588480714825,4.23081122457936));
#131752=CARTESIAN_POINT('Ctrl Pts',(-21.2939990418858,19.2087851537695,
4.23329008725203));
#131753=CARTESIAN_POINT('',(-21.2939989159607,19.2133559031925,4.16670989022851));
#131754=CARTESIAN_POINT('Ctrl Pts',(-17.174464231106,17.180864983421,3.88329345071054));
#131755=CARTESIAN_POINT('Ctrl Pts',(-17.2411551865789,17.1296334497189,
3.887463318742));
#131756=CARTESIAN_POINT('Ctrl Pts',(-17.3103645228761,17.0816983118158,
3.89163318677346));
#131757=CARTESIAN_POINT('Ctrl Pts',(-17.3817276205797,17.0373028242515,
3.89580305480492));
#131758=CARTESIAN_POINT('Ctrl Pts',(-17.4531659153384,16.9928605560677,
3.89997731672912));
#131759=CARTESIAN_POINT('Ctrl Pts',(-17.5267621115622,16.9519656290489,
3.90415157865332));
#131760=CARTESIAN_POINT('Ctrl Pts',(-17.6021248960207,16.914816481857,3.90832584057752));
#131761=CARTESIAN_POINT('Ctrl Pts',(-17.6775292444906,16.8776468462026,
3.91250240468669));
#131762=CARTESIAN_POINT('Ctrl Pts',(-17.7547016988925,16.8442272867161,
3.91667896879587));
#131763=CARTESIAN_POINT('Ctrl Pts',(-17.8332310067443,16.814708026807,3.92085553290504));
#131764=CARTESIAN_POINT('Ctrl Pts',(-17.9118959414518,16.7851377846021,
3.92503931029895));
#131765=CARTESIAN_POINT('Ctrl Pts',(-17.991921971515,16.7594814360342,3.92922308769286));
#131766=CARTESIAN_POINT('Ctrl Pts',(-18.0728829745269,16.7378392129444,
3.93340686508677));
#131767=CARTESIAN_POINT('Ctrl Pts',(-18.1312147786055,16.7222461512216,
3.936421245766));
#131768=CARTESIAN_POINT('Ctrl Pts',(-18.1900316496069,16.708735796216,3.93943562644523));
#131769=CARTESIAN_POINT('Ctrl Pts',(-18.249172131343,16.6973289917387,3.94245000712447));
#131770=CARTESIAN_POINT('Ctrl Pts',(-18.3312723437006,16.6814937965827,
3.94663464151747));
#131771=CARTESIAN_POINT('Ctrl Pts',(-18.4143019582715,16.6696556340513,
3.95081927591047));
#131772=CARTESIAN_POINT('Ctrl Pts',(-18.4978371529754,16.6619164176738,
3.95500391030347));
#131773=CARTESIAN_POINT('Ctrl Pts',(-18.5812534456692,16.6541882171128,
3.95918258838736));
#131774=CARTESIAN_POINT('Ctrl Pts',(-18.6651734349295,16.6505474159413,
3.96336126647126));
#131775=CARTESIAN_POINT('Ctrl Pts',(-18.7491632186827,16.651044907269,3.96753994455515));
#131776=CARTESIAN_POINT('Ctrl Pts',(-18.8346584589486,16.6515513157714,
3.9717935224406));
#131777=CARTESIAN_POINT('Ctrl Pts',(-18.9202255470369,16.6563459251098,
3.97604710032605));
#131778=CARTESIAN_POINT('Ctrl Pts',(-19.0054014154824,16.6654271230872,
3.9803006782115));
#131779=CARTESIAN_POINT('Ctrl Pts',(-19.0889259835097,16.6743322643211,
3.98447179218939));
#131780=CARTESIAN_POINT('Ctrl Pts',(-19.172073887133,16.6873592186152,3.98864290616729));
#131781=CARTESIAN_POINT('Ctrl Pts',(-19.2544103550733,16.7044539576675,
3.99281402014518));
#131782=CARTESIAN_POINT('Ctrl Pts',(-19.3367191942165,16.7215429604151,
3.9969837344655));
#131783=CARTESIAN_POINT('Ctrl Pts',(-19.4182166883867,16.7426969435999,
4.00115344878582));
#131784=CARTESIAN_POINT('Ctrl Pts',(-19.4984772632642,16.76781058574,4.00532316310613));
#131785=CARTESIAN_POINT('Ctrl Pts',(-19.5787349821259,16.792923334229,4.00949272905011));
#131786=CARTESIAN_POINT('Ctrl Pts',(-19.6577554304202,16.8219953233345,
4.0136622949941));
#131787=CARTESIAN_POINT('Ctrl Pts',(-19.7351285466043,16.8548714735452,
4.01783186093808));
#131788=CARTESIAN_POINT('Ctrl Pts',(-19.8152220061057,16.8889035086413,
4.02214802367707));
#131789=CARTESIAN_POINT('Ctrl Pts',(-19.8935496523609,16.9270119844455,
4.02646418641605));
#131790=CARTESIAN_POINT('Ctrl Pts',(-19.9696814080995,16.9689715751853,
4.03078034915504));
#131791=CARTESIAN_POINT('Ctrl Pts',(-20.0433331799005,17.0095643366689,
4.03495591334666));
#131792=CARTESIAN_POINT('Ctrl Pts',(-20.1149295504513,17.0537608783676,
4.03913147753828));
#131793=CARTESIAN_POINT('Ctrl Pts',(-20.1841097633269,17.1013124225839,
4.04330704172991));
#131794=CARTESIAN_POINT('Ctrl Pts',(-20.2567841042975,17.1512656822575,
4.04769350374257));
#131795=CARTESIAN_POINT('Ctrl Pts',(-20.3267913293723,17.2049214186621,
4.05207996575524));
#131796=CARTESIAN_POINT('Ctrl Pts',(-20.3937533178432,17.2619440942066,
4.0564664277679));
#131797=CARTESIAN_POINT('Ctrl Pts',(-20.4607153063142,17.318966769751,4.06085288978057));
#131798=CARTESIAN_POINT('Ctrl Pts',(-20.5246316886729,17.3793559306721,
4.06523935179323));
#131799=CARTESIAN_POINT('Ctrl Pts',(-20.5851713910718,17.4427340469043,
4.0696258138059));
#131800=CARTESIAN_POINT('Ctrl Pts',(-20.6421808499863,17.5024164036099,
4.07375648865202));
#131801=CARTESIAN_POINT('Ctrl Pts',(-20.6964202744402,17.5649836670307,
4.07788716349815));
#131802=CARTESIAN_POINT('Ctrl Pts',(-20.7475781317949,17.6301448177783,
4.08201783834428));
#131803=CARTESIAN_POINT('Ctrl Pts',(-20.7986699217384,17.6952218166719,
4.08614317866296));
#131804=CARTESIAN_POINT('Ctrl Pts',(-20.8466877493677,17.7628856907895,
4.09026851898165));
#131805=CARTESIAN_POINT('Ctrl Pts',(-20.8913569516644,17.8328088002366,
4.09439385930033));
#131806=CARTESIAN_POINT('Ctrl Pts',(-20.9359826817961,17.9026638603613,
4.09851518482883));
#131807=CARTESIAN_POINT('Ctrl Pts',(-20.977265999821,17.9747733973533,4.10263651035733));
#131808=CARTESIAN_POINT('Ctrl Pts',(-21.0149735460515,18.0487781269426,
4.10675783588582));
#131809=CARTESIAN_POINT('Ctrl Pts',(-21.0526563884393,18.122734372836,4.1108764613559));
#131810=CARTESIAN_POINT('Ctrl Pts',(-21.0867678956213,18.1985829265156,
4.11499508682597));
#131811=CARTESIAN_POINT('Ctrl Pts',(-21.117119754579,18.2759383788566,4.11911371229604));
#131812=CARTESIAN_POINT('Ctrl Pts',(-21.1474714047475,18.3532932990728,
4.12323230943427));
#131813=CARTESIAN_POINT('Ctrl Pts',(-21.174063267692,18.4321546644581,4.1273509065725));
#131814=CARTESIAN_POINT('Ctrl Pts',(-21.1967549321189,18.5121165016086,
4.13146950371073));
#131815=CARTESIAN_POINT('Ctrl Pts',(-21.2194452848828,18.5920737166658,
4.13558786277863));
#131816=CARTESIAN_POINT('Ctrl Pts',(-21.238235765403,18.6731308198826,4.13970622184654));
#131817=CARTESIAN_POINT('Ctrl Pts',(-21.2530362470694,18.7548680169614,
4.14382458091445));
#131818=CARTESIAN_POINT('Ctrl Pts',(-21.2678499327185,18.8366781344066,
4.14794661410212));
#131819=CARTESIAN_POINT('Ctrl Pts',(-21.2786664327327,18.9191690901919,
4.1520686472898));
#131820=CARTESIAN_POINT('Ctrl Pts',(-21.2854471635996,19.001913005284,4.15619068047748));
#131821=CARTESIAN_POINT('Ctrl Pts',(-21.2912151852698,19.0722990307271,
4.15969708372782));
#131822=CARTESIAN_POINT('Ctrl Pts',(-21.2940637843831,19.1428678239492,
4.16320348697816));
#131823=CARTESIAN_POINT('Ctrl Pts',(-21.2939989159607,19.2133559031925,
4.16670989022851));
#131824=CARTESIAN_POINT('Ctrl Pts',(-21.2939117877142,19.2133565885178,
4.16670992830965));
#131825=CARTESIAN_POINT('Ctrl Pts',(-21.2957664845097,19.4149927548523,
4.17674049236887));
#131826=CARTESIAN_POINT('Ctrl Pts',(-21.1817726734028,20.4667260333026,
4.22916299198858));
#131827=CARTESIAN_POINT('Ctrl Pts',(-19.7309870503076,22.0692002142848,
4.32397742716876));
#131828=CARTESIAN_POINT('Ctrl Pts',(-16.8703561207535,21.5963978986231,
4.4511532338502));
#131829=CARTESIAN_POINT('Ctrl Pts',(-15.78678603666,19.0907282468595,4.57089385988457));
#131830=CARTESIAN_POINT('Ctrl Pts',(-16.6213792270115,17.6125716320285,
4.64824255035846));
#131831=CARTESIAN_POINT('Ctrl Pts',(-17.1735447493682,17.1796894255362,
4.68319930527188));
#131832=CARTESIAN_POINT('Origin',(-18.734,19.211,-1.76670989022852));
#131833=CARTESIAN_POINT('',(-17.174464231106,17.180864983421,5.54983331567207));
#131834=CARTESIAN_POINT('',(-17.174464231106,17.180864983421,5.4833696502435));
#131835=CARTESIAN_POINT('',(-17.174464231106,17.180864983421,-1.76670989022852));
#131836=CARTESIAN_POINT('',(-21.2938494844892,19.2121967450766,5.03329016024561));
#131837=CARTESIAN_POINT('Ctrl Pts',(-21.2939997202205,19.2121968587231,
5.03329016239734));
#131838=CARTESIAN_POINT('Ctrl Pts',(-21.293956476523,19.3046921979846,5.03786858507676));
#131839=CARTESIAN_POINT('Ctrl Pts',(-21.2888961385951,19.397020737122,5.04244700775617));
#131840=CARTESIAN_POINT('Ctrl Pts',(-21.2788976615039,19.4886614709891,
5.04702543043559));
#131841=CARTESIAN_POINT('Ctrl Pts',(-21.2688681118718,19.5805869992732,
5.0516180816045));
#131842=CARTESIAN_POINT('Ctrl Pts',(-21.2538698091613,19.6718201549447,
5.0562107327734));
#131843=CARTESIAN_POINT('Ctrl Pts',(-21.234032630531,19.7618510200409,5.0608033839423));
#131844=CARTESIAN_POINT('Ctrl Pts',(-21.2141037578168,19.8522980379506,
5.06541726388317));
#131845=CARTESIAN_POINT('Ctrl Pts',(-21.1892913049467,19.9415313457699,
5.07003114382404));
#131846=CARTESIAN_POINT('Ctrl Pts',(-21.1597755903685,20.0290542678652,
5.07464502376491));
#131847=CARTESIAN_POINT('Ctrl Pts',(-21.1363775884239,20.0984363421481,
5.07830258629969));
#131848=CARTESIAN_POINT('Ctrl Pts',(-21.1100249393954,20.1667439285117,
5.08196014883446));
#131849=CARTESIAN_POINT('Ctrl Pts',(-21.0808281256645,20.233740313369,5.08561771136923));
#131850=CARTESIAN_POINT('Ctrl Pts',(-21.0474239145965,20.3103911904541,
5.08980234576228));
#131851=CARTESIAN_POINT('Ctrl Pts',(-21.010198294198,20.3855464442561,5.09398698015533));
#131852=CARTESIAN_POINT('Ctrl Pts',(-20.9693070771846,20.458798970463,5.09817161454838));
#131853=CARTESIAN_POINT('Ctrl Pts',(-20.9284740637573,20.5319472307656,
5.10235029263232));
#131854=CARTESIAN_POINT('Ctrl Pts',(-20.8839860396698,20.6031977447538,
5.10652897071627));
#131855=CARTESIAN_POINT('Ctrl Pts',(-20.8360465870688,20.6721639695093,
5.11070764880021));
#131856=CARTESIAN_POINT('Ctrl Pts',(-20.7872478542335,20.7423663642784,
5.11496122668565));
#131857=CARTESIAN_POINT('Ctrl Pts',(-20.734872934752,20.8102013305707,5.11921480457108));
#131858=CARTESIAN_POINT('Ctrl Pts',(-20.6791852047648,20.8752879916541,
5.12346838245652));
#131859=CARTESIAN_POINT('Ctrl Pts',(-20.6245770900892,20.9391128208062,
5.12763949643447));
#131860=CARTESIAN_POINT('Ctrl Pts',(-20.5667837820758,21.0002945906743,
5.13181061041242));
#131861=CARTESIAN_POINT('Ctrl Pts',(-20.506095860174,21.0585054160554,5.13598172439037));
#131862=CARTESIAN_POINT('Ctrl Pts',(-20.4454283026905,21.1166967082319,
5.14015143871074));
#131863=CARTESIAN_POINT('Ctrl Pts',(-20.381868392088,21.1719187176573,5.14432115303111));
#131864=CARTESIAN_POINT('Ctrl Pts',(-20.3157437934276,21.2238801683044,
5.14849086735148));
#131865=CARTESIAN_POINT('Ctrl Pts',(-20.2496215477641,21.2758397699402,
5.15266043329552));
#131866=CARTESIAN_POINT('Ctrl Pts',(-20.180935157738,21.3245387599149,5.15682999923957));
#131867=CARTESIAN_POINT('Ctrl Pts',(-20.1100445342432,21.3697268098996,
5.16099956518361));
#131868=CARTESIAN_POINT('Ctrl Pts',(-20.0366614838794,21.4165036159763,
5.16531572792253));
#131869=CARTESIAN_POINT('Ctrl Pts',(-19.9609167591477,21.4595177156538,
5.16963189066145));
#131870=CARTESIAN_POINT('Ctrl Pts',(-19.8832395142306,21.4985420299813,
5.17394805340037));
#131871=CARTESIAN_POINT('Ctrl Pts',(-19.8080925973965,21.5362951313742,
5.17812361759205));
#131872=CARTESIAN_POINT('Ctrl Pts',(-19.7311375805024,21.5703142429021,
5.18229918178373));
#131873=CARTESIAN_POINT('Ctrl Pts',(-19.6527837251099,21.6004427104396,
5.18647474597541));
#131874=CARTESIAN_POINT('Ctrl Pts',(-19.5704724027502,21.6320928952488,
5.19086120798796));
#131875=CARTESIAN_POINT('Ctrl Pts',(-19.4866177726057,21.6594488930308,
5.1952476700005));
#131876=CARTESIAN_POINT('Ctrl Pts',(-19.4017104542221,21.6823888300554,
5.19963413201304));
#131877=CARTESIAN_POINT('Ctrl Pts',(-19.3168031358385,21.7053287670799,
5.20402059402558));
#131878=CARTESIAN_POINT('Ctrl Pts',(-19.2308437124363,21.723852595477,5.20840705603813));
#131879=CARTESIAN_POINT('Ctrl Pts',(-19.1443308019265,21.7379009939035,
5.21279351805067));
#131880=CARTESIAN_POINT('Ctrl Pts',(-19.0617984786721,21.7513030046936,
5.21697815244372));
#131881=CARTESIAN_POINT('Ctrl Pts',(-18.9784552815194,21.7606822624715,
5.22116278683677));
#131882=CARTESIAN_POINT('Ctrl Pts',(-18.894727859237,21.7659494232303,5.22534742122981));
#131883=CARTESIAN_POINT('Ctrl Pts',(-18.8111196125767,21.7712090868378,
5.22952609931376));
#131884=CARTESIAN_POINT('Ctrl Pts',(-18.7271286822943,21.7723682508116,
5.23370477739771));
#131885=CARTESIAN_POINT('Ctrl Pts',(-18.6431902849674,21.7693888671693,
5.23788345548165));
#131886=CARTESIAN_POINT('Ctrl Pts',(-18.5577473521938,21.7663560802164,
5.24213703336709));
#131887=CARTESIAN_POINT('Ctrl Pts',(-18.4723593301117,21.7590348421053,
5.24639061125252));
#131888=CARTESIAN_POINT('Ctrl Pts',(-18.3874890362873,21.7474404491387,
5.25064418913796));
#131889=CARTESIAN_POINT('Ctrl Pts',(-18.3042641187194,21.7360708361043,
5.25481530311591));
#131890=CARTESIAN_POINT('Ctrl Pts',(-18.2215375109945,21.7205923416799,
5.25898641709386));
#131891=CARTESIAN_POINT('Ctrl Pts',(-18.1397421978238,21.7010718191555,
5.26315753107181));
#131892=CARTESIAN_POINT('Ctrl Pts',(-18.0579743318604,21.681557846931,5.26732724539218));
#131893=CARTESIAN_POINT('Ctrl Pts',(-17.977137586906,21.6580046470219,5.27149695971256));
#131894=CARTESIAN_POINT('Ctrl Pts',(-17.8976542388868,21.6305300717015,
5.27566667403293));
#131895=CARTESIAN_POINT('Ctrl Pts',(-17.8181737192262,21.6030564740444,
5.27983623997698));
#131896=CARTESIAN_POINT('Ctrl Pts',(-17.7400469352591,21.5716619295132,
5.28400580592102));
#131897=CARTESIAN_POINT('Ctrl Pts',(-17.6636791864352,21.536513568236,5.28817537186506));
#131898=CARTESIAN_POINT('Ctrl Pts',(-17.5846264417725,21.5001294339366,
5.29249153460398));
#131899=CARTESIAN_POINT('Ctrl Pts',(-17.5074592081876,21.4597228236283,
5.29680769734291));
#131900=CARTESIAN_POINT('Ctrl Pts',(-17.4326007161618,21.4155316745344,
5.30112386008182));
#131901=CARTESIAN_POINT('Ctrl Pts',(-17.3601807316399,21.3727800474741,
5.3052994242735));
#131902=CARTESIAN_POINT('Ctrl Pts',(-17.2899217514085,21.3264869565081,
5.30947498846518));
#131903=CARTESIAN_POINT('Ctrl Pts',(-17.2221770223173,21.276911731936,5.31365055265686));
#131904=CARTESIAN_POINT('Ctrl Pts',(-17.1510106680076,21.2248325806246,
5.3180370146694));
#131905=CARTESIAN_POINT('Ctrl Pts',(-17.0826196821851,21.1691313897079,
5.32242347668194));
#131906=CARTESIAN_POINT('Ctrl Pts',(-17.0173721044249,21.1101547246429,
5.32680993869448));
#131907=CARTESIAN_POINT('Ctrl Pts',(-16.9521245266647,21.0511780595779,
5.33119640070702));
#131908=CARTESIAN_POINT('Ctrl Pts',(-16.890020712904,20.9889263848495,5.33558286271956));
#131909=CARTESIAN_POINT('Ctrl Pts',(-16.8313804354228,20.923786849695,5.3399693247321));
#131910=CARTESIAN_POINT('Ctrl Pts',(-16.7754382840342,20.8616444811128,
5.34415395912515));
#131911=CARTESIAN_POINT('Ctrl Pts',(-16.7224397206527,20.7966428559978,
5.3483385935182));
#131912=CARTESIAN_POINT('Ctrl Pts',(-16.6726908063355,20.7290923582293,
5.35252322791125));
#131913=CARTESIAN_POINT('Ctrl Pts',(-16.62301270344,20.6616380102332,5.35670190599519));
#131914=CARTESIAN_POINT('Ctrl Pts',(-16.5765753324319,20.5916423631924,
5.36088058407914));
#131915=CARTESIAN_POINT('Ctrl Pts',(-16.533646260122,20.5194507707226,5.36505926216308));
#131916=CARTESIAN_POINT('Ctrl Pts',(-16.4899477150434,20.4459651958411,
5.36931284004852));
#131917=CARTESIAN_POINT('Ctrl Pts',(-16.4498848008427,20.3702045348862,
5.37356641793395));
#131918=CARTESIAN_POINT('Ctrl Pts',(-16.4136951701205,20.2925662237873,
5.37781999581939));
#131919=CARTESIAN_POINT('Ctrl Pts',(-16.378207146008,20.2164330828478,5.38199110979734));
#131920=CARTESIAN_POINT('Ctrl Pts',(-16.3464437665668,20.1384948820615,
5.38616222377529));
#131921=CARTESIAN_POINT('Ctrl Pts',(-16.3185831851716,20.0591518794675,
5.39033333775325));
#131922=CARTESIAN_POINT('Ctrl Pts',(-16.2907319526636,19.9798355011842,
5.39450305207362));
#131923=CARTESIAN_POINT('Ctrl Pts',(-16.2667810695588,19.8991156909808,
5.398672766394));
#131924=CARTESIAN_POINT('Ctrl Pts',(-16.2468600106956,19.8174113072848,
5.40284248071437));
#131925=CARTESIAN_POINT('Ctrl Pts',(-16.2269396607092,19.7357098309814,
5.40701204665841));
#131926=CARTESIAN_POINT('Ctrl Pts',(-16.2110489579958,19.6530242979865,
5.41118161260246));
#131927=CARTESIAN_POINT('Ctrl Pts',(-16.1992667534716,19.5697859653661,
5.4153511785465));
#131928=CARTESIAN_POINT('Ctrl Pts',(-16.1870703011713,19.4836210756562,
5.41966734128542));
#131929=CARTESIAN_POINT('Ctrl Pts',(-16.1792767060087,19.3968643124029,
5.42398350402434));
#131930=CARTESIAN_POINT('Ctrl Pts',(-16.1759149870658,19.3100003363692,
5.42829966676326));
#131931=CARTESIAN_POINT('Ctrl Pts',(-16.1726627757638,19.2259659452183,
5.43247523095494));
#131932=CARTESIAN_POINT('Ctrl Pts',(-16.1735580857934,19.1418316894465,
5.43665079514662));
#131933=CARTESIAN_POINT('Ctrl Pts',(-16.1785740672325,19.0580349643242,
5.4408263593383));
#131934=CARTESIAN_POINT('Ctrl Pts',(-16.1838433939698,18.9700058658238,
5.44521282135084));
#131935=CARTESIAN_POINT('Ctrl Pts',(-16.1936605371381,18.8823498716686,
5.44959928336338));
#131936=CARTESIAN_POINT('Ctrl Pts',(-16.2079333028748,18.7955640342065,
5.45398574537592));
#131937=CARTESIAN_POINT('Ctrl Pts',(-16.2222060686114,18.7087781967444,
5.45837220738847));
#131938=CARTESIAN_POINT('Ctrl Pts',(-16.2409342590202,18.6228630666792,
5.46275866940101));
#131939=CARTESIAN_POINT('Ctrl Pts',(-16.2639654295305,18.5382970784325,
5.46714513141355));
#131940=CARTESIAN_POINT('Ctrl Pts',(-16.2859330287302,18.4576363176213,
5.47132902816135));
#131941=CARTESIAN_POINT('Ctrl Pts',(-16.3118967078484,18.3779026599609,
5.47551292490916));
#131942=CARTESIAN_POINT('Ctrl Pts',(-16.3417612031297,18.2995212351631,
5.47969682165697));
#131943=CARTESIAN_POINT('Ctrl Pts',(-16.3715858706168,18.2212443411543,
5.48387513868956));
#131944=CARTESIAN_POINT('Ctrl Pts',(-16.4053008633433,18.1443165254295,
5.48805345572216));
#131945=CARTESIAN_POINT('Ctrl Pts',(-16.4427606710955,18.0691495992551,
5.49223177275476));
#131946=CARTESIAN_POINT('Ctrl Pts',(-16.480181764331,17.9940603577085,5.4964057715184));
#131947=CARTESIAN_POINT('Ctrl Pts',(-16.521339781578,17.9207288006143,5.50057977028204));
#131948=CARTESIAN_POINT('Ctrl Pts',(-16.5660409635037,17.8495472406015,
5.50475376904568));
#131949=CARTESIAN_POINT('Ctrl Pts',(-16.6107117825475,17.7784140300327,
5.50892493265764));
#131950=CARTESIAN_POINT('Ctrl Pts',(-16.6589207423336,17.7094283045759,
5.5130960962696));
#131951=CARTESIAN_POINT('Ctrl Pts',(-16.7104285669956,17.6429570619627,
5.51726725988155));
#131952=CARTESIAN_POINT('Ctrl Pts',(-16.7619153763033,17.5765129398254,
5.52143672164565));
#131953=CARTESIAN_POINT('Ctrl Pts',(-16.8166980925828,17.5125816237491,
5.52560618340975));
#131954=CARTESIAN_POINT('Ctrl Pts',(-16.8744954343627,17.4514992837814,
5.52977564517385));
#131955=CARTESIAN_POINT('Ctrl Pts',(-16.93230250686,17.3904066600364,5.53394580890543));
#131956=CARTESIAN_POINT('Ctrl Pts',(-16.9931249059284,17.332164308163,5.538115972637));
#131957=CARTESIAN_POINT('Ctrl Pts',(-17.0566432414669,17.2770728285162,
5.54228613636858));
#131958=CARTESIAN_POINT('Ctrl Pts',(-17.0949618222409,17.2438379004453,
5.54480186280308));
#131959=CARTESIAN_POINT('Ctrl Pts',(-17.1342608277126,17.2117489616349,
5.54731758923758));
#131960=CARTESIAN_POINT('Ctrl Pts',(-17.174464231106,17.180864983421,5.54983331567207));
#131961=CARTESIAN_POINT('Ctrl Pts',(-17.1762220704533,17.183189381701,4.74997346579241));
#131962=CARTESIAN_POINT('Ctrl Pts',(-17.6117180491967,16.8534335803771,
4.77707100986373));
#131963=CARTESIAN_POINT('Ctrl Pts',(-18.9946006232268,16.3463963590632,
4.84656048949553));
#131964=CARTESIAN_POINT('Ctrl Pts',(-20.9008595855074,17.3473638996065,
4.94099937082188));
#131965=CARTESIAN_POINT('Ctrl Pts',(-21.288210327615,18.7088774717577,5.00834070807693));
#131966=CARTESIAN_POINT('Ctrl Pts',(-21.2903253369841,19.2121940792196,
5.0332901097715));
#131967=CARTESIAN_POINT('',(-21.2942631007509,19.2101644346482,4.96670989022851));
#131968=CARTESIAN_POINT('Ctrl Pts',(-17.1735447493682,17.1796894255362,
4.68319930527188));
#131969=CARTESIAN_POINT('Ctrl Pts',(-17.2909884427537,17.0876168801257,
4.69063448591894));
#131970=CARTESIAN_POINT('Ctrl Pts',(-18.1310916530698,16.5418820156488,
4.74046160212649));
#131971=CARTESIAN_POINT('Ctrl Pts',(-20.2331956221585,16.5812273615557,
4.8326806538945));
#131972=CARTESIAN_POINT('Ctrl Pts',(-21.2762381336493,18.2701494254144,
4.91974900156631));
#131973=CARTESIAN_POINT('Ctrl Pts',(-21.2980949765117,19.1644257538227,
4.96442541367765));
#131974=CARTESIAN_POINT('Ctrl Pts',(-21.2979002687903,19.210163247625,4.96670989022851));
#131975=CARTESIAN_POINT('Ctrl Pts',(-21.2939998636668,19.210164520558,4.96670989022851));
#131976=CARTESIAN_POINT('Ctrl Pts',(-21.2940269378475,19.2931227545131,
4.97085977152528));
#131977=CARTESIAN_POINT('Ctrl Pts',(-21.2900172964774,19.3762448671897,
4.97500965282206));
#131978=CARTESIAN_POINT('Ctrl Pts',(-21.2819493183893,19.4591013319584,
4.97915953411883));
#131979=CARTESIAN_POINT('Ctrl Pts',(-21.273892503302,19.5418431550195,4.98330367356457));
#131980=CARTESIAN_POINT('Ctrl Pts',(-21.2617885455564,19.6243195978693,
4.9874478130103));
#131981=CARTESIAN_POINT('Ctrl Pts',(-21.2456678375727,19.7061006702713,
4.99159195245604));
#131982=CARTESIAN_POINT('Ctrl Pts',(-21.2295645603718,19.787793315532,4.99573161098226));
#131983=CARTESIAN_POINT('Ctrl Pts',(-21.2094532518121,19.8687916269892,
4.99987126950847));
#131984=CARTESIAN_POINT('Ctrl Pts',(-21.185415992005,19.9486717658566,5.00401092803468));
#131985=CARTESIAN_POINT('Ctrl Pts',(-21.1613926712712,20.0285055826756,
5.00814818599593));
#131986=CARTESIAN_POINT('Ctrl Pts',(-21.1334480518402,20.1072220663071,
5.01228544395718));
#131987=CARTESIAN_POINT('Ctrl Pts',(-21.1017147974227,20.1844097996556,
5.01642270191842));
#131988=CARTESIAN_POINT('Ctrl Pts',(-21.0699900384709,20.2615768686961,
5.02055885227398));
#131989=CARTESIAN_POINT('Ctrl Pts',(-21.0344788364884,20.3372155671953,
5.02469500262954));
#131990=CARTESIAN_POINT('Ctrl Pts',(-20.9953624823965,20.4109332161455,
5.02883115298509));
#131991=CARTESIAN_POINT('Ctrl Pts',(-20.9562443890678,20.4846541428155,
5.03296748724698));
#131992=CARTESIAN_POINT('Ctrl Pts',(-20.9135210465748,20.5564534375451,
5.03710382150886));
#131993=CARTESIAN_POINT('Ctrl Pts',(-20.8674196102005,20.6259631680054,
5.04124015577075));
#131994=CARTESIAN_POINT('Ctrl Pts',(-20.8212714994521,20.6955432720466,
5.04538067777227));
#131995=CARTESIAN_POINT('Ctrl Pts',(-20.7717387262307,20.7628287929985,
5.0495211997738));
#131996=CARTESIAN_POINT('Ctrl Pts',(-20.7190913321275,20.8274814886389,
5.05366172177532));
#131997=CARTESIAN_POINT('Ctrl Pts',(-20.6664157771977,20.8921687666814,
5.05780445852126));
#131998=CARTESIAN_POINT('Ctrl Pts',(-20.6106225991445,20.9542200685987,
5.0619471952672));
#131999=CARTESIAN_POINT('Ctrl Pts',(-20.5520199344765,21.0133327988598,
5.06608993201314));
#132000=CARTESIAN_POINT('Ctrl Pts',(-20.4933173061603,21.0725463628324,
5.07023973538449));
#132001=CARTESIAN_POINT('Ctrl Pts',(-20.4317959684764,21.1288110311776,
5.07438953875584));
#132002=CARTESIAN_POINT('Ctrl Pts',(-20.3677981562815,21.181863664623,5.07853934212718));
#132003=CARTESIAN_POINT('Ctrl Pts',(-20.3241391698325,21.218055905033,5.08137031717058));
#132004=CARTESIAN_POINT('Ctrl Pts',(-20.2793283343472,21.252754156268,5.08420129221397));
#132005=CARTESIAN_POINT('Ctrl Pts',(-20.2334815623284,21.2858867545572,
5.08703226725737));
#132006=CARTESIAN_POINT('Ctrl Pts',(-20.165712692572,21.3348620398235,5.09121690165042));
#132007=CARTESIAN_POINT('Ctrl Pts',(-20.0954157767524,21.38060482739,5.09540153604347));
#132008=CARTESIAN_POINT('Ctrl Pts',(-20.0229321512534,21.4228440065848,
5.09958617043652));
#132009=CARTESIAN_POINT('Ctrl Pts',(-19.9505516972236,21.4650230635362,
5.10376484852047));
#132010=CARTESIAN_POINT('Ctrl Pts',(-19.8759911100092,21.5037081881331,
5.10794352660441));
#132011=CARTESIAN_POINT('Ctrl Pts',(-19.7996223782742,21.5386702831203,
5.11212220468836));
#132012=CARTESIAN_POINT('Ctrl Pts',(-19.7218847919081,21.5742590485333,
5.1163757825738));
#132013=CARTESIAN_POINT('Ctrl Pts',(-19.6422739922293,21.6059897185086,
5.12062936045924));
#132014=CARTESIAN_POINT('Ctrl Pts',(-19.5612105522306,21.6336685085414,
5.12488293834467));
#132015=CARTESIAN_POINT('Ctrl Pts',(-19.4817186851986,21.6608106912187,
5.12905405232262));
#132016=CARTESIAN_POINT('Ctrl Pts',(-19.4008304551545,21.684056543659,5.13322516630057));
#132017=CARTESIAN_POINT('Ctrl Pts',(-19.3189628776792,21.7032717411505,
5.13739628027853));
#132018=CARTESIAN_POINT('Ctrl Pts',(-19.2371227716601,21.7224804907969,
5.1415659945989));
#132019=CARTESIAN_POINT('Ctrl Pts',(-19.1543044183624,21.7376611666004,
5.14573570891928));
#132020=CARTESIAN_POINT('Ctrl Pts',(-19.0709381209924,21.7487298324727,
5.14990542323965));
#132021=CARTESIAN_POINT('Ctrl Pts',(-18.9875747901528,21.7597981044745,
5.15407498918371));
#132022=CARTESIAN_POINT('Ctrl Pts',(-18.9036640101513,21.7667545977696,
5.15824455512777));
#132023=CARTESIAN_POINT('Ctrl Pts',(-18.8196429975834,21.7695670358552,
5.16241412107182));
#132024=CARTESIAN_POINT('Ctrl Pts',(-18.732667909865,21.7724783557944,5.16673028381074));
#132025=CARTESIAN_POINT('Ctrl Pts',(-18.6455752209298,21.7709487709587,
5.17104644654966));
#132026=CARTESIAN_POINT('Ctrl Pts',(-18.5588499153528,21.7650012623035,
5.17536260928857));
#132027=CARTESIAN_POINT('Ctrl Pts',(-18.4749496774831,21.7592474931172,
5.17953817348025));
#132028=CARTESIAN_POINT('Ctrl Pts',(-18.3913937177399,21.7493593099809,
5.18371373767193));
#132029=CARTESIAN_POINT('Ctrl Pts',(-18.3086140512028,21.7354101874628,
5.18788930186361));
#132030=CARTESIAN_POINT('Ctrl Pts',(-18.2216533804991,21.7207565279272,
5.19227576387614));
#132031=CARTESIAN_POINT('Ctrl Pts',(-18.135550055063,21.7016210383819,5.19666222588868));
#132032=CARTESIAN_POINT('Ctrl Pts',(-18.0507884164761,21.6781485427794,
5.20104868790121));
#132033=CARTESIAN_POINT('Ctrl Pts',(-17.9660267778892,21.654676047177,5.20543514991374));
#132034=CARTESIAN_POINT('Ctrl Pts',(-17.8826073525322,21.6268668011753,
5.20982161192628));
#132035=CARTESIAN_POINT('Ctrl Pts',(-17.8009895271363,21.5949235427183,
5.21420807393881));
#132036=CARTESIAN_POINT('Ctrl Pts',(-17.7231270588735,21.5644500409342,
5.21839270833185));
#132037=CARTESIAN_POINT('Ctrl Pts',(-17.6466142262365,21.5301011627873,
5.2225773427249));
#132038=CARTESIAN_POINT('Ctrl Pts',(-17.5718637493069,21.4920171710938,
5.22676197711794));
#132039=CARTESIAN_POINT('Ctrl Pts',(-17.497219670429,21.4539873872488,5.23094065520188));
#132040=CARTESIAN_POINT('Ctrl Pts',(-17.4243333709912,21.4122332570933,
5.23511933328581));
#132041=CARTESIAN_POINT('Ctrl Pts',(-17.3535988359381,21.366943558226,5.23929801136975));
#132042=CARTESIAN_POINT('Ctrl Pts',(-17.2815964351799,21.3208420740556,
5.24355158925519));
#132043=CARTESIAN_POINT('Ctrl Pts',(-17.2118241472901,21.2710772000459,
5.24780516714062));
#132044=CARTESIAN_POINT('Ctrl Pts',(-17.1446725625544,21.2178976796495,
5.25205874502606));
#132045=CARTESIAN_POINT('Ctrl Pts',(-17.0788228423243,21.1657491480273,
5.25622985900401));
#132046=CARTESIAN_POINT('Ctrl Pts',(-17.0154934944018,21.1103174864337,
5.26040097298197));
#132047=CARTESIAN_POINT('Ctrl Pts',(-16.9550231872364,21.051880631559,5.26457208695992));
#132048=CARTESIAN_POINT('Ctrl Pts',(-16.8945731714665,20.9934633857354,
5.26874180128029));
#132049=CARTESIAN_POINT('Ctrl Pts',(-16.836980621644,20.9320432687888,5.27291151560067));
#132050=CARTESIAN_POINT('Ctrl Pts',(-16.7825490297002,20.8679366646061,
5.27708122992104));
#132051=CARTESIAN_POINT('Ctrl Pts',(-16.7281193746661,20.8038323416116,
5.28125079586508));
#132052=CARTESIAN_POINT('Ctrl Pts',(-16.6768507509731,20.7370420726798,
5.28542036180911));
#132053=CARTESIAN_POINT('Ctrl Pts',(-16.6290069551027,20.6679160171177,
5.28958992775315));
#132054=CARTESIAN_POINT('Ctrl Pts',(-16.5794810303911,20.596359574718,5.29390609049207));
#132055=CARTESIAN_POINT('Ctrl Pts',(-16.5336255484986,20.5223004707795,
5.298222253231));
#132056=CARTESIAN_POINT('Ctrl Pts',(-16.4916836990305,20.4461589397347,
5.30253841596993));
#132057=CARTESIAN_POINT('Ctrl Pts',(-16.4511081008974,20.3724977110551,
5.30671398016161));
#132058=CARTESIAN_POINT('Ctrl Pts',(-16.4141952418313,20.296888085941,5.31088954435328));
#132059=CARTESIAN_POINT('Ctrl Pts',(-16.3811171829165,20.2197330910965,
5.31506510854496));
#132060=CARTESIAN_POINT('Ctrl Pts',(-16.3463684298815,20.138681180881,5.31945157055751));
#132061=CARTESIAN_POINT('Ctrl Pts',(-16.3158522513523,20.0559242327781,
5.32383803257006));
#132062=CARTESIAN_POINT('Ctrl Pts',(-16.2897090382154,19.9719478918678,
5.3282244945826));
#132063=CARTESIAN_POINT('Ctrl Pts',(-16.2635658250786,19.8879715509576,
5.33261095659515));
#132064=CARTESIAN_POINT('Ctrl Pts',(-16.2417956472861,19.8027763982257,
5.3369974186077));
#132065=CARTESIAN_POINT('Ctrl Pts',(-16.2244766916358,19.7168584434174,
5.34138388062024));
#132066=CARTESIAN_POINT('Ctrl Pts',(-16.2079546068078,19.6348937010709,
5.3455685150133));
#132067=CARTESIAN_POINT('Ctrl Pts',(-16.1954216323758,19.5519661209785,
5.34975314940634));
#132068=CARTESIAN_POINT('Ctrl Pts',(-16.1869832270606,19.4684986570164,
5.3539377837994));
#132069=CARTESIAN_POINT('Ctrl Pts',(-16.1785568327709,19.3851499986582,
5.35811646188333));
#132070=CARTESIAN_POINT('Ctrl Pts',(-16.1742134770096,19.3012634366144,
5.36229513996727));
#132071=CARTESIAN_POINT('Ctrl Pts',(-16.174007684269,19.2172724316078,5.36647381805121));
#132072=CARTESIAN_POINT('Ctrl Pts',(-16.1737982028414,19.1317759481995,
5.37072739593665));
#132073=CARTESIAN_POINT('Ctrl Pts',(-16.177876170323,19.0461717133521,5.37498097382208));
#132074=CARTESIAN_POINT('Ctrl Pts',(-16.1862438519479,18.9609227917969,
5.37923455170752));
#132075=CARTESIAN_POINT('Ctrl Pts',(-16.1944493097363,18.8773265869357,
5.38340566568547));
#132076=CARTESIAN_POINT('Ctrl Pts',(-16.2067795899915,18.7940725203434,
5.38757677966342));
#132077=CARTESIAN_POINT('Ctrl Pts',(-16.2231843067498,18.7115958004499,
5.39174789364137));
#132078=CARTESIAN_POINT('Ctrl Pts',(-16.2395835187469,18.6291467564163,
5.39591760796174));
#132079=CARTESIAN_POINT('Ctrl Pts',(-16.2600543622649,18.5474749918557,
5.40008732228212));
#132080=CARTESIAN_POINT('Ctrl Pts',(-16.2844950829501,18.467006948051,5.40425703660249));
#132081=CARTESIAN_POINT('Ctrl Pts',(-16.3089349339296,18.3865417676445,
5.40842660254654));
#132082=CARTESIAN_POINT('Ctrl Pts',(-16.3373442466934,18.307280662759,5.41259616849058));
#132083=CARTESIAN_POINT('Ctrl Pts',(-16.3695713807106,18.2296349790802,
5.41676573443463));
#132084=CARTESIAN_POINT('Ctrl Pts',(-16.4029315810032,18.1492593689496,
5.42108189717355));
#132085=CARTESIAN_POINT('Ctrl Pts',(-16.4403828646778,18.0706153771455,
5.42539805991247));
#132086=CARTESIAN_POINT('Ctrl Pts',(-16.4817035150009,17.9941349525684,
5.42971422265139));
#132087=CARTESIAN_POINT('Ctrl Pts',(-16.5216781494859,17.9201458697775,
5.43388978684307));
#132088=CARTESIAN_POINT('Ctrl Pts',(-16.5652736482195,17.8481819408652,
5.43806535103475));
#132089=CARTESIAN_POINT('Ctrl Pts',(-16.6122442629255,17.7786059926852,
5.44224091522643));
#132090=CARTESIAN_POINT('Ctrl Pts',(-16.6615872517183,17.7055159287636,
5.44662737723897));
#132091=CARTESIAN_POINT('Ctrl Pts',(-16.714654919849,17.6350618855121,5.45101383925151));
#132092=CARTESIAN_POINT('Ctrl Pts',(-16.7711149075846,17.5676247799199,
5.45540030126405));
#132093=CARTESIAN_POINT('Ctrl Pts',(-16.8275748953203,17.5001876743276,
5.45978676327659));
#132094=CARTESIAN_POINT('Ctrl Pts',(-16.8874267520075,17.4357678796896,
5.46417322528913));
#132095=CARTESIAN_POINT('Ctrl Pts',(-16.9502957329765,17.3746996193972,
5.46855968730167));
#132096=CARTESIAN_POINT('Ctrl Pts',(-17.0102748276238,17.3164384720464,
5.47274451766097));
#132097=CARTESIAN_POINT('Ctrl Pts',(-17.0732230246168,17.2610106350511,
5.47692934802027));
#132098=CARTESIAN_POINT('Ctrl Pts',(-17.1388417266104,17.2087337632481,
5.48111417837957));
#132099=CARTESIAN_POINT('Ctrl Pts',(-17.1506304271778,17.1993419836248,
5.48186600233421));
#132100=CARTESIAN_POINT('Ctrl Pts',(-17.1625052169379,17.1900518159241,
5.48261782628886));
#132101=CARTESIAN_POINT('Ctrl Pts',(-17.174464231106,17.180864983421,5.4833696502435));
#132102=CARTESIAN_POINT('Origin',(-18.734,19.211,-1.76670989022852));
#132103=CARTESIAN_POINT('',(-17.1721129728022,17.177834880393,6.34984102388608));
#132104=CARTESIAN_POINT('',(-17.174464231106,17.180864983421,6.28334279855885));
#132105=CARTESIAN_POINT('',(-17.174464231106,17.180864983421,-1.76670989022852));
#132106=CARTESIAN_POINT('',(-21.2939994369002,19.2126979607666,5.8332901097715));
#132107=CARTESIAN_POINT('Ctrl Pts',(-21.2967674808324,19.2126997967162,
5.8332901097715));
#132108=CARTESIAN_POINT('Ctrl Pts',(-21.2975540827487,19.3154768305114,
5.83841759033361));
#132109=CARTESIAN_POINT('Ctrl Pts',(-21.2452321516418,20.267165082075,5.8859370064562));
#132110=CARTESIAN_POINT('Ctrl Pts',(-20.0538051929683,21.9352257637231,
5.97584835813928));
#132111=CARTESIAN_POINT('Ctrl Pts',(-17.1577427696511,21.7953190404615,
6.10302416482071));
#132112=CARTESIAN_POINT('Ctrl Pts',(-15.7364333538251,19.3340467515488,
6.22768838673632));
#132113=CARTESIAN_POINT('Ctrl Pts',(-16.5413043832607,17.6674200121866,
6.30996067309144));
#132114=CARTESIAN_POINT('Ctrl Pts',(-17.1721129728022,17.177834880393,6.34984102388608));
#132115=CARTESIAN_POINT('Ctrl Pts',(-17.174464231106,17.180864983421,5.54983331567207));
#132116=CARTESIAN_POINT('Ctrl Pts',(-17.2411774753928,17.1296163276052,
5.55400789438973));
#132117=CARTESIAN_POINT('Ctrl Pts',(-17.3103823939862,17.0816880702098,
5.55818247310739));
#132118=CARTESIAN_POINT('Ctrl Pts',(-17.3817083728383,17.0373147985257,
5.56235705182505));
#132119=CARTESIAN_POINT('Ctrl Pts',(-17.4530770005447,16.992914994164,5.56653412670193));
#132120=CARTESIAN_POINT('Ctrl Pts',(-17.5265688111888,16.9520746303608,
5.57071120157881));
#132121=CARTESIAN_POINT('Ctrl Pts',(-17.6017888279468,16.9149821730052,
5.57488827645568));
#132122=CARTESIAN_POINT('Ctrl Pts',(-17.6771347920593,16.8778276085527,
5.57907234536889));
#132123=CARTESIAN_POINT('Ctrl Pts',(-17.7542143174781,16.8444336617759,
5.5832564142821));
#132124=CARTESIAN_POINT('Ctrl Pts',(-17.8326130703151,16.8149404007844,
5.58744048319531));
#132125=CARTESIAN_POINT('Ctrl Pts',(-17.8755871141844,16.7987737572368,
5.58973396816186));
#132126=CARTESIAN_POINT('Ctrl Pts',(-17.9189572740205,16.7837782551377,
5.59202745312842));
#132127=CARTESIAN_POINT('Ctrl Pts',(-17.9626538344085,16.7699704850561,
5.59432093809497));
#132128=CARTESIAN_POINT('Ctrl Pts',(-18.0423814681728,16.7447771786174,
5.59850557248802));
#132129=CARTESIAN_POINT('Ctrl Pts',(-18.1234930456338,16.7234471296282,
5.60269020688107));
#132130=CARTESIAN_POINT('Ctrl Pts',(-18.2055793173493,16.7061304261206,
5.60687484127411));
#132131=CARTESIAN_POINT('Ctrl Pts',(-18.2875487494172,16.688838370797,5.61105351935805));
#132132=CARTESIAN_POINT('Ctrl Pts',(-18.3704896737369,16.6755484082766,
5.61523219744199));
#132133=CARTESIAN_POINT('Ctrl Pts',(-18.4539769469564,16.6663611081798,
5.61941087552594));
#132134=CARTESIAN_POINT('Ctrl Pts',(-18.5389606695472,16.6570091323315,
5.62366445341137));
#132135=CARTESIAN_POINT('Ctrl Pts',(-18.6245100605659,16.6519084913031,
5.62791803129681));
#132136=CARTESIAN_POINT('Ctrl Pts',(-18.7101649534091,16.6511109612809,
5.63217160918225));
#132137=CARTESIAN_POINT('Ctrl Pts',(-18.7941592590127,16.6503288929346,
5.6363427231602));
#132138=CARTESIAN_POINT('Ctrl Pts',(-18.87825453103,16.6536845805936,5.64051383713815));
#132139=CARTESIAN_POINT('Ctrl Pts',(-18.9620126684401,16.6611744720411,
5.6446849511161));
#132140=CARTESIAN_POINT('Ctrl Pts',(-19.0457426999984,16.6686618501832,
5.64885466543648));
#132141=CARTESIAN_POINT('Ctrl Pts',(-19.1291353638019,16.6802806360297,
5.65302437975685));
#132142=CARTESIAN_POINT('Ctrl Pts',(-19.2117557819362,16.6959752659613,
5.65719409407723));
#132143=CARTESIAN_POINT('Ctrl Pts',(-19.2943732600815,16.7116693374106,
5.66136366002127));
#132144=CARTESIAN_POINT('Ctrl Pts',(-19.3762180954027,16.7314388778862,
5.66553322596532));
#132145=CARTESIAN_POINT('Ctrl Pts',(-19.4568650837658,16.7551771092621,
5.66970279190936));
#132146=CARTESIAN_POINT('Ctrl Pts',(-19.5403475207509,16.7797499475689,
5.67401895464828));
#132147=CARTESIAN_POINT('Ctrl Pts',(-19.6225458049916,16.808575598709,5.6783351173872));
#132148=CARTESIAN_POINT('Ctrl Pts',(-19.7030067527824,16.8414798137466,
5.68265128012612));
#132149=CARTESIAN_POINT('Ctrl Pts',(-19.7808466936618,16.8733121774403,
5.6868268443178));
#132150=CARTESIAN_POINT('Ctrl Pts',(-19.8570603406959,16.9089612248342,
5.69100240850948));
#132151=CARTESIAN_POINT('Ctrl Pts',(-19.9312606656525,16.9482214208011,
5.69517797270116));
#132152=CARTESIAN_POINT('Ctrl Pts',(-20.0092086726281,16.9894645559341,
5.6995644347137));
#132153=CARTESIAN_POINT('Ctrl Pts',(-20.0849341253746,17.0346929255447,
5.70395089672625));
#132154=CARTESIAN_POINT('Ctrl Pts',(-20.1580227463385,17.0836168145089,
5.70833735873879));
#132155=CARTESIAN_POINT('Ctrl Pts',(-20.2311113673024,17.132540703473,5.71272382075133));
#132156=CARTESIAN_POINT('Ctrl Pts',(-20.3015627371329,17.1851597036451,
5.71711028276387));
#132157=CARTESIAN_POINT('Ctrl Pts',(-20.3690044710744,17.2411369642621,
5.72149674477641));
#132158=CARTESIAN_POINT('Ctrl Pts',(-20.4324580482224,17.2938040179914,
5.72562381401755));
#132159=CARTESIAN_POINT('Ctrl Pts',(-20.4934979978141,17.3496514870446,
5.72975088325869));
#132160=CARTESIAN_POINT('Ctrl Pts',(-20.5517814829092,17.4084267059583,
5.73387795249984));
#132161=CARTESIAN_POINT('Ctrl Pts',(-20.6102782700972,17.4674170265802,
5.73802012571949));
#132162=CARTESIAN_POINT('Ctrl Pts',(-20.6659979620834,17.5293563204315,
5.74216229893914));
#132163=CARTESIAN_POINT('Ctrl Pts',(-20.7186255971237,17.5939467419898,
5.74630447215879));
#132164=CARTESIAN_POINT('Ctrl Pts',(-20.7709257203662,17.658135205051,5.75042086784547));
#132165=CARTESIAN_POINT('Ctrl Pts',(-20.8201718394843,17.7249415391099,
5.75453726353214));
#132166=CARTESIAN_POINT('Ctrl Pts',(-20.8660914253506,17.7940362905331,
5.75865365921881));
#132167=CARTESIAN_POINT('Ctrl Pts',(-20.9119829684087,17.8630888462171,
5.76276754104799));
#132168=CARTESIAN_POINT('Ctrl Pts',(-20.9545517475123,17.9344266527042,
5.76688142287717));
#132169=CARTESIAN_POINT('Ctrl Pts',(-20.9935669693931,18.0076891046668,
5.77099530470634));
#132170=CARTESIAN_POINT('Ctrl Pts',(-21.0325708263853,18.0809302157382,
5.77510798818763));
#132171=CARTESIAN_POINT('Ctrl Pts',(-21.0680229592547,18.1560944409463,
5.77922067166891));
#132172=CARTESIAN_POINT('Ctrl Pts',(-21.0997379788824,18.2327956168196,
5.7833333551502));
#132173=CARTESIAN_POINT('Ctrl Pts',(-21.1318415000295,18.3104363640289,
5.78749641803531));
#132174=CARTESIAN_POINT('Ctrl Pts',(-21.1601155043873,18.3896515290328,
5.79165948092042));
#132175=CARTESIAN_POINT('Ctrl Pts',(-21.1844181339266,18.4700202641611,
5.79582254380553));
#132176=CARTESIAN_POINT('Ctrl Pts',(-21.2084475698835,18.5494855487958,
5.79993880837768));
#132177=CARTESIAN_POINT('Ctrl Pts',(-21.2285944016388,18.6300781193823,
5.80405507294983));
#132178=CARTESIAN_POINT('Ctrl Pts',(-21.2447724368935,18.7113783730305,
5.80817133752198));
#132179=CARTESIAN_POINT('Ctrl Pts',(-21.2612263672264,18.7940650953984,
5.81235779956356));
#132180=CARTESIAN_POINT('Ctrl Pts',(-21.2735747867911,18.8774833595966,
5.81654426160515));
#132181=CARTESIAN_POINT('Ctrl Pts',(-21.281781944964,18.9611857471732,5.82073072364674));
#132182=CARTESIAN_POINT('Ctrl Pts',(-21.2899891031369,19.0448881347499,
5.82491718568833));
#132183=CARTESIAN_POINT('Ctrl Pts',(-21.2940550344004,19.1288741338655,
5.82910364772991));
#132184=CARTESIAN_POINT('Ctrl Pts',(-21.2939994369002,19.2126979607666,
5.8332901097715));
#132185=CARTESIAN_POINT('',(-21.2939992944986,19.2090994299067,5.76670989019962));
#132186=CARTESIAN_POINT('Ctrl Pts',(-17.174464231106,17.180864983421,5.4833696502435));
#132187=CARTESIAN_POINT('Ctrl Pts',(-17.2409183890944,17.1298153559192,
5.48754740496134));
#132188=CARTESIAN_POINT('Ctrl Pts',(-17.3099760635813,17.0819596693814,
5.49172515967919));
#132189=CARTESIAN_POINT('Ctrl Pts',(-17.381296247198,17.037571244058,5.49590291439703));
#132190=CARTESIAN_POINT('Ctrl Pts',(-17.4525396221523,16.9932306230924,
5.50007616985905));
#132191=CARTESIAN_POINT('Ctrl Pts',(-17.5260402745971,16.9523500835238,
5.50424942532106));
#132192=CARTESIAN_POINT('Ctrl Pts',(-17.6014266254566,16.9151608176365,
5.50842268078308));
#132193=CARTESIAN_POINT('Ctrl Pts',(-17.6767687012082,16.8779933933524,
5.51259348525319));
#132194=CARTESIAN_POINT('Ctrl Pts',(-17.7539938650333,16.8445131416642,
5.5167642897233));
#132195=CARTESIAN_POINT('Ctrl Pts',(-17.8327052167042,16.8149057377466,
5.5209350941934));
#132196=CARTESIAN_POINT('Ctrl Pts',(-17.911393952278,16.785306840911,5.52510470026815));
#132197=CARTESIAN_POINT('Ctrl Pts',(-17.9915675972202,16.7595787434778,
5.52927430634291));
#132198=CARTESIAN_POINT('Ctrl Pts',(-18.0728097832131,16.7378587793607,
5.53344391241766));
#132199=CARTESIAN_POINT('Ctrl Pts',(-18.1540529965122,16.716138540595,5.53761357121702));
#132200=CARTESIAN_POINT('Ctrl Pts',(-18.2363643329242,16.698426653361,5.54178323001638));
#132201=CARTESIAN_POINT('Ctrl Pts',(-18.3193141232468,16.6848100578893,
5.54595288881574));
#132202=CARTESIAN_POINT('Ctrl Pts',(-18.4023475185942,16.6711797382623,
5.55012675021075));
#132203=CARTESIAN_POINT('Ctrl Pts',(-18.4860201982849,16.661653030515,5.55430061160575));
#132204=CARTESIAN_POINT('Ctrl Pts',(-18.5698946588579,16.6562652902877,
5.55847447300076));
#132205=CARTESIAN_POINT('Ctrl Pts',(-18.6538097229503,16.6508749418623,
5.56265035495674));
#132206=CARTESIAN_POINT('Ctrl Pts',(-18.7379263019653,16.6496275592858,
5.56682623691272));
#132207=CARTESIAN_POINT('Ctrl Pts',(-18.8218066258234,16.6525063032203,
5.57100211886871));
#132208=CARTESIAN_POINT('Ctrl Pts',(-18.9058385141806,16.6553902487964,
5.57518554628264));
#132209=CARTESIAN_POINT('Ctrl Pts',(-18.9896328347449,16.6624151806863,
5.57936897369658));
#132210=CARTESIAN_POINT('Ctrl Pts',(-19.0727567278495,16.6735122898156,
5.58355240111052));
#132211=CARTESIAN_POINT('Ctrl Pts',(-19.1534486270523,16.6842847257286,
5.58761343206805));
#132212=CARTESIAN_POINT('Ctrl Pts',(-19.2335084226815,16.698894184328,5.59167446302558));
#132213=CARTESIAN_POINT('Ctrl Pts',(-19.3125527301388,16.7172324209243,
5.59573549398311));
#132214=CARTESIAN_POINT('Ctrl Pts',(-19.3940028670669,16.7361288086572,
5.59992012837615));
#132215=CARTESIAN_POINT('Ctrl Pts',(-19.4746778298125,16.7590549809083,
5.60410476276919));
#132216=CARTESIAN_POINT('Ctrl Pts',(-19.5541489559097,16.7859318174286,
5.60828939716224));
#132217=CARTESIAN_POINT('Ctrl Pts',(-19.6335069646957,16.8127703980989,
5.61246807524619));
#132218=CARTESIAN_POINT('Ctrl Pts',(-19.7116641083501,16.8435483273113,
5.61664675333013));
#132219=CARTESIAN_POINT('Ctrl Pts',(-19.7882032486925,16.8781357711075,
5.62082543141408));
#132220=CARTESIAN_POINT('Ctrl Pts',(-19.8661142981178,16.9133431699762,
5.62507900929951));
#132221=CARTESIAN_POINT('Ctrl Pts',(-19.9423482986085,16.9524978888715,
5.62933258718495));
#132222=CARTESIAN_POINT('Ctrl Pts',(-20.0164828014234,16.995410267208,5.63358616507039));
#132223=CARTESIAN_POINT('Ctrl Pts',(-20.0891800622395,17.0374907053539,
5.63775727904834));
#132224=CARTESIAN_POINT('Ctrl Pts',(-20.15985808817,17.0831841629369,5.64192839302629));
#132225=CARTESIAN_POINT('Ctrl Pts',(-20.2281415862035,17.1322645862503,
5.64609950700424));
#132226=CARTESIAN_POINT('Ctrl Pts',(-20.2964021710499,17.1813285401536,
5.65026922132462));
#132227=CARTESIAN_POINT('Ctrl Pts',(-20.3622694505382,17.2337769343483,
5.65443893564499));
#132228=CARTESIAN_POINT('Ctrl Pts',(-20.4253973801086,17.289340586222,5.65860864996537));
#132229=CARTESIAN_POINT('Ctrl Pts',(-20.4885230633163,17.3449022609025,
5.66277821590942));
#132230=CARTESIAN_POINT('Ctrl Pts',(-20.5489092456572,17.4035786682711,
5.66694778185346));
#132231=CARTESIAN_POINT('Ctrl Pts',(-20.6062442778987,17.4650614661805,
5.67111734779751));
#132232=CARTESIAN_POINT('Ctrl Pts',(-20.6655951391432,17.5287059234172,
5.67543351053643));
#132233=CARTESIAN_POINT('Ctrl Pts',(-20.7216759416723,17.5953574026464,
5.67974967327535));
#132234=CARTESIAN_POINT('Ctrl Pts',(-20.7741852955296,17.6646352435778,
5.68406583601427));
#132235=CARTESIAN_POINT('Ctrl Pts',(-20.8249841627081,17.7316563661277,
5.68824140020596));
#132236=CARTESIAN_POINT('Ctrl Pts',(-20.8724404611874,17.8011349549806,
5.69241696439764));
#132237=CARTESIAN_POINT('Ctrl Pts',(-20.9163256700512,17.872697093392,5.69659252858933));
#132238=CARTESIAN_POINT('Ctrl Pts',(-20.9624274164875,17.9478736652916,
5.70097899060187));
#132239=CARTESIAN_POINT('Ctrl Pts',(-21.004587562026,18.0253492855826,5.7053654526144));
#132240=CARTESIAN_POINT('Ctrl Pts',(-21.0425969786767,18.1046637084301,
5.70975191462694));
#132241=CARTESIAN_POINT('Ctrl Pts',(-21.0806063953274,18.1839781312776,
5.71413837663948));
#132242=CARTESIAN_POINT('Ctrl Pts',(-21.1144649298774,18.2651307919131,
5.71852483865201));
#132243=CARTESIAN_POINT('Ctrl Pts',(-21.1440235064309,18.3476421955815,
5.72291130066455));
#132244=CARTESIAN_POINT('Ctrl Pts',(-21.1768030234133,18.4391447059575,
5.72777574688617));
#132245=CARTESIAN_POINT('Ctrl Pts',(-21.2043967060816,18.5325974942123,
5.73264019310779));
#132246=CARTESIAN_POINT('Ctrl Pts',(-21.2266026211952,18.6274486545204,
5.73750463932941));
#132247=CARTESIAN_POINT('Ctrl Pts',(-21.2488226674981,18.722360175309,5.74237218114112));
#132248=CARTESIAN_POINT('Ctrl Pts',(-21.2656479288592,18.818671733481,5.74723972295282));
#132249=CARTESIAN_POINT('Ctrl Pts',(-21.2769239065508,18.9158085274062,
5.75210726476452));
#132250=CARTESIAN_POINT('Ctrl Pts',(-21.2881998842425,19.0129453213313,
5.75697480657622));
#132251=CARTESIAN_POINT('Ctrl Pts',(-21.2939263955806,19.1109072194806,
5.76184234838792));
#132252=CARTESIAN_POINT('Ctrl Pts',(-21.2939992944986,19.2090994299067,
5.76670989019962));
#132253=CARTESIAN_POINT('Ctrl Pts',(-21.293999294499,19.2090994304895,5.76670989022851));
#132254=CARTESIAN_POINT('Ctrl Pts',(-21.2940618231948,19.2933233519321,
5.77088500205647));
#132255=CARTESIAN_POINT('Ctrl Pts',(-21.2899635861128,19.3775880720651,
5.77506011388443));
#132256=CARTESIAN_POINT('Ctrl Pts',(-21.2817191504239,19.4614538491683,
5.77923522571239));
#132257=CARTESIAN_POINT('Ctrl Pts',(-21.2734754980237,19.5453116583388,
5.78340994087068));
#132258=CARTESIAN_POINT('Ctrl Pts',(-21.2610864747303,19.6287701442277,
5.78758465602897));
#132259=CARTESIAN_POINT('Ctrl Pts',(-21.2446185572459,19.7113943045362,
5.79175937118726));
#132260=CARTESIAN_POINT('Ctrl Pts',(-21.2281473245847,19.794035098017,5.79593492676264));
#132261=CARTESIAN_POINT('Ctrl Pts',(-21.2075956572653,19.8758407835678,
5.80011048233803));
#132262=CARTESIAN_POINT('Ctrl Pts',(-21.1830809475491,19.956387491411,5.80428603791341));
#132263=CARTESIAN_POINT('Ctrl Pts',(-21.1585369190256,20.0370305305357,
5.80846658731945));
#132264=CARTESIAN_POINT('Ctrl Pts',(-21.1300205198885,20.1164111473511,
5.8126471367255));
#132265=CARTESIAN_POINT('Ctrl Pts',(-21.0976986239764,20.1941219736187,
5.81682768613154));
#132266=CARTESIAN_POINT('Ctrl Pts',(-21.0653559283573,20.2718828081662,
5.82101092579446));
#132267=CARTESIAN_POINT('Ctrl Pts',(-21.0292030575738,20.347971299817,5.82519416545738));
#132268=CARTESIAN_POINT('Ctrl Pts',(-20.9894534545796,20.4220035979404,
5.8293774051203));
#132269=CARTESIAN_POINT('Ctrl Pts',(-20.9496320042093,20.4961697093846,
5.83356820598562));
#132270=CARTESIAN_POINT('Ctrl Pts',(-20.906201076148,20.5682718138337,5.83775900685095));
#132271=CARTESIAN_POINT('Ctrl Pts',(-20.8594180036074,20.6379542073737,
5.84194980771627));
#132272=CARTESIAN_POINT('Ctrl Pts',(-20.8291383592868,20.6830550948788,
5.84466224092617));
#132273=CARTESIAN_POINT('Ctrl Pts',(-20.7974553185202,20.7271429654288,
5.84737467413607));
#132274=CARTESIAN_POINT('Ctrl Pts',(-20.7644472985012,20.770129169764,5.85008710734597));
#132275=CARTESIAN_POINT('Ctrl Pts',(-20.7135238341689,20.8364465811685,
5.85427174173902));
#132276=CARTESIAN_POINT('Ctrl Pts',(-20.6592531496868,20.9003899294851,
5.85845637613207));
#132277=CARTESIAN_POINT('Ctrl Pts',(-20.6018847443057,20.9616017771012,
5.86264101052512));
#132278=CARTESIAN_POINT('Ctrl Pts',(-20.5445979957491,21.0227264972285,
5.86681968860906));
#132279=CARTESIAN_POINT('Ctrl Pts',(-20.4842225962896,21.0811271065652,
5.87099836669299));
#132280=CARTESIAN_POINT('Ctrl Pts',(-20.4210494366145,21.1364776546142,
5.87517704477693));
#132281=CARTESIAN_POINT('Ctrl Pts',(-20.3567439434538,21.1928203214575,
5.87943062266237));
#132282=CARTESIAN_POINT('Ctrl Pts',(-20.28953969747,21.2460021244011,5.8836842005478));
#132283=CARTESIAN_POINT('Ctrl Pts',(-20.2197842460679,21.2957170489388,
5.88793777843324));
#132284=CARTESIAN_POINT('Ctrl Pts',(-20.1513811402078,21.3444681526537,
5.89210889241119));
#132285=CARTESIAN_POINT('Ctrl Pts',(-20.0805252582506,21.3898853234968,
5.89628000638914));
#132286=CARTESIAN_POINT('Ctrl Pts',(-20.0075777510546,21.4317205389284,
5.9004511203671));
#132287=CARTESIAN_POINT('Ctrl Pts',(-19.9346547220992,21.4735417161496,
5.90462083468747));
#132288=CARTESIAN_POINT('Ctrl Pts',(-19.8596418605524,21.5117830963986,
5.90879054900784));
#132289=CARTESIAN_POINT('Ctrl Pts',(-19.7829274662088,21.5462411375772,
5.91296026332822));
#132290=CARTESIAN_POINT('Ctrl Pts',(-19.7062158016926,21.5806979525908,
5.91712982927226));
#132291=CARTESIAN_POINT('Ctrl Pts',(-19.6278031447569,21.6113715084927,
5.92129939521631));
#132292=CARTESIAN_POINT('Ctrl Pts',(-19.5480992000004,21.6381057852015,
5.92546896116035));
#132293=CARTESIAN_POINT('Ctrl Pts',(-19.4655929628717,21.6657800060991,
5.92978512389927));
#132294=CARTESIAN_POINT('Ctrl Pts',(-19.3817034451245,21.6892326159302,
5.93410128663819));
#132295=CARTESIAN_POINT('Ctrl Pts',(-19.2969019322698,21.708346875115,5.93841744937711));
#132296=CARTESIAN_POINT('Ctrl Pts',(-19.2148628197768,21.7268384893174,
5.9425930135688));
#132297=CARTESIAN_POINT('Ctrl Pts',(-19.13197068837,21.7412700216398,5.94676857776048));
#132298=CARTESIAN_POINT('Ctrl Pts',(-19.0486605152119,21.751588270493,5.95094414195216));
#132299=CARTESIAN_POINT('Ctrl Pts',(-18.9611425432588,21.7624276695664,
5.9553306039647));
#132300=CARTESIAN_POINT('Ctrl Pts',(-18.8731637715283,21.7687272994046,
5.95971706597724));
#132301=CARTESIAN_POINT('Ctrl Pts',(-18.7852297301452,21.7704873538951,
5.96410352798978));
#132302=CARTESIAN_POINT('Ctrl Pts',(-18.6972956887621,21.7722474083857,
5.96848999000232));
#132303=CARTESIAN_POINT('Ctrl Pts',(-18.6094069552492,21.7694679818952,
5.97287645201486));
#132304=CARTESIAN_POINT('Ctrl Pts',(-18.5220617179689,21.7622119011579,
5.9772629140274));
#132305=CARTESIAN_POINT('Ctrl Pts',(-18.4387353645324,21.7552896834514,
5.98144754842046));
#132306=CARTESIAN_POINT('Ctrl Pts',(-18.3555934356672,21.7442679479862,
5.98563218281351));
#132307=CARTESIAN_POINT('Ctrl Pts',(-18.2730715290521,21.7291630099478,
5.98981681720656));
#132308=CARTESIAN_POINT('Ctrl Pts',(-18.1906670821569,21.7140795719191,
5.9939954952905));
#132309=CARTESIAN_POINT('Ctrl Pts',(-18.108881353184,21.6949245577665,5.99817417337445));
#132310=CARTESIAN_POINT('Ctrl Pts',(-18.0281458685303,21.6717661297017,
6.0023528514584));
#132311=CARTESIAN_POINT('Ctrl Pts',(-17.9459632583377,21.6481926034575,
6.00660642934383));
#132312=CARTESIAN_POINT('Ctrl Pts',(-17.8648693945433,21.6204707691484,
6.01086000722927));
#132313=CARTESIAN_POINT('Ctrl Pts',(-17.7853097077372,21.5887272192929,
6.0151135851147));
#132314=CARTESIAN_POINT('Ctrl Pts',(-17.7072924407079,21.5575990800938,
6.01928469909265));
#132315=CARTESIAN_POINT('Ctrl Pts',(-17.6307508424367,21.5226039497267,
6.0234558130706));
#132316=CARTESIAN_POINT('Ctrl Pts',(-17.5560889447388,21.4839112490138,
6.02762692704856));
#132317=CARTESIAN_POINT('Ctrl Pts',(-17.4814521005618,21.4452315320103,
6.03179664136893));
#132318=CARTESIAN_POINT('Ctrl Pts',(-17.4086941123782,21.4028569203158,
6.0359663556893));
#132319=CARTESIAN_POINT('Ctrl Pts',(-17.3381963061957,21.3570037391305,
6.04013607000967));
#132320=CARTESIAN_POINT('Ctrl Pts',(-17.2677010086276,21.3111521895981,
6.04430563595371));
#132321=CARTESIAN_POINT('Ctrl Pts',(-17.1994661183239,21.261822568227,6.04847520189776));
#132322=CARTESIAN_POINT('Ctrl Pts',(-17.133844588811,21.2092749210363,6.0526447678418));
#132323=CARTESIAN_POINT('Ctrl Pts',(-17.0659158872733,21.1548797633949,
6.05696093058072));
#132324=CARTESIAN_POINT('Ctrl Pts',(-17.0007881489953,21.0970364076612,
6.06127709331964));
#132325=CARTESIAN_POINT('Ctrl Pts',(-16.9388146313976,21.0360779414469,
6.06559325605856));
#132326=CARTESIAN_POINT('Ctrl Pts',(-16.8788598946172,20.9771051908578,
6.06976882025024));
#132327=CARTESIAN_POINT('Ctrl Pts',(-16.8218573212167,20.9152175410394,
6.07394438444192));
#132328=CARTESIAN_POINT('Ctrl Pts',(-16.7680870902015,20.8507519419374,
6.0781199486336));
#132329=CARTESIAN_POINT('Ctrl Pts',(-16.7116010526442,20.7830303386771,
6.08250641064614));
#132330=CARTESIAN_POINT('Ctrl Pts',(-16.6586828203999,20.7124639847437,
6.08689287265868));
#132331=CARTESIAN_POINT('Ctrl Pts',(-16.6096058643084,20.6394780559179,
6.09127933467122));
#132332=CARTESIAN_POINT('Ctrl Pts',(-16.5605289082169,20.5664921270921,
6.09566579668377));
#132333=CARTESIAN_POINT('Ctrl Pts',(-16.5152934615327,20.4910871600581,
6.10005225869631));
#132334=CARTESIAN_POINT('Ctrl Pts',(-16.4741163568267,20.4137160593082,
6.10443872070885));
#132335=CARTESIAN_POINT('Ctrl Pts',(-16.4348338717473,20.3399049175952,
6.1086233551019));
#132336=CARTESIAN_POINT('Ctrl Pts',(-16.3990982578627,20.2640298565514,
6.11280798949495));
#132337=CARTESIAN_POINT('Ctrl Pts',(-16.3671315774457,20.1864659759906,
6.116992623888));
#132338=CARTESIAN_POINT('Ctrl Pts',(-16.3352103976415,20.1090124980131,
6.12117130197195));
#132339=CARTESIAN_POINT('Ctrl Pts',(-16.3070476692931,20.0298753969617,
6.12534998005591));
#132340=CARTESIAN_POINT('Ctrl Pts',(-16.2828196558214,19.949454413158,6.12952865813987));
#132341=CARTESIAN_POINT('Ctrl Pts',(-16.2581573726207,19.8675919410174,
6.1337822360253));
#132342=CARTESIAN_POINT('Ctrl Pts',(-16.2375724777941,19.7843995318231,
6.13803581391074));
#132343=CARTESIAN_POINT('Ctrl Pts',(-16.2211996301976,19.70032024434,6.14228939179617));
#132344=CARTESIAN_POINT('Ctrl Pts',(-16.2051442022007,19.6178709979119,
6.14646050577412));
#132345=CARTESIAN_POINT('Ctrl Pts',(-16.1931390533221,19.5345694264037,
6.15063161975207));
#132346=CARTESIAN_POINT('Ctrl Pts',(-16.18526042222,19.4508469609104,6.15480273373002));
#132347=CARTESIAN_POINT('Ctrl Pts',(-16.1773844348688,19.367152589299,6.1589724480504));
#132348=CARTESIAN_POINT('Ctrl Pts',(-16.1736322583368,19.2830380618257,
6.16314216237077));
#132349=CARTESIAN_POINT('Ctrl Pts',(-16.1740284019004,19.1989411060445,
6.16731187669115));
#132350=CARTESIAN_POINT('Ctrl Pts',(-16.1744245313676,19.114847142794,6.17148144263519));
#132351=CARTESIAN_POINT('Ctrl Pts',(-16.1789686844146,19.0307712100163,
6.17565100857923));
#132352=CARTESIAN_POINT('Ctrl Pts',(-16.187633250542,18.9471508437488,6.17982057452327));
#132353=CARTESIAN_POINT('Ctrl Pts',(-16.1966024521254,18.8605904885602,
6.18413673726219));
#132354=CARTESIAN_POINT('Ctrl Pts',(-16.2099871509034,18.7745188559838,
6.18845290000111));
#132355=CARTESIAN_POINT('Ctrl Pts',(-16.2276984844483,18.689413273613,6.19276906274002));
#132356=CARTESIAN_POINT('Ctrl Pts',(-16.2448328731659,18.6070799966363,
6.1969446269317));
#132357=CARTESIAN_POINT('Ctrl Pts',(-16.2660161808879,18.5256512422047,
6.20112019112338));
#132358=CARTESIAN_POINT('Ctrl Pts',(-16.291116741615,18.4455449811373,6.20529575531506));
#132359=CARTESIAN_POINT('Ctrl Pts',(-16.3174850719935,18.361392743258,6.2096822173276));
#132360=CARTESIAN_POINT('Ctrl Pts',(-16.3481765728436,18.2787006554451,
6.21406867934013));
#132361=CARTESIAN_POINT('Ctrl Pts',(-16.3829817631982,18.1979288029831,
6.21845514135267));
#132362=CARTESIAN_POINT('Ctrl Pts',(-16.4177869535528,18.1171569505211,
6.22284160336521));
#132363=CARTESIAN_POINT('Ctrl Pts',(-16.4567055084016,18.0383058200372,
6.22722806537775));
#132364=CARTESIAN_POINT('Ctrl Pts',(-16.4994739740983,17.9618028820207,
6.23161452739028));
#132365=CARTESIAN_POINT('Ctrl Pts',(-16.5415036475325,17.8866214732604,
6.23592521665433));
#132366=CARTESIAN_POINT('Ctrl Pts',(-16.5874123973693,17.8134194400118,
6.24023590591838));
#132367=CARTESIAN_POINT('Ctrl Pts',(-16.6369860604329,17.7426224813552,
6.24454659518243));
#132368=CARTESIAN_POINT('Ctrl Pts',(-16.6850336937779,17.6740048706875,
6.2487245881816));
#132369=CARTESIAN_POINT('Ctrl Pts',(-16.7365236311432,17.6076468533131,
6.25290258118077));
#132370=CARTESIAN_POINT('Ctrl Pts',(-16.7912139344855,17.5439120288232,
6.25708057417994));
#132371=CARTESIAN_POINT('Ctrl Pts',(-16.8485097468532,17.4771408039058,
6.26145761157643));
#132372=CARTESIAN_POINT('Ctrl Pts',(-16.9093182143514,17.4132493917059,
6.26583464897291));
#132373=CARTESIAN_POINT('Ctrl Pts',(-16.973310725425,17.3526207926269,6.2702116863694));
#132374=CARTESIAN_POINT('Ctrl Pts',(-17.0373032364986,17.291992193548,6.27458872376588));
#132375=CARTESIAN_POINT('Ctrl Pts',(-17.1044794046939,17.2346268461436,
6.27896576116237));
#132376=CARTESIAN_POINT('Ctrl Pts',(-17.174464231106,17.180864983421,6.28334279855885));
#132377=CARTESIAN_POINT('Origin',(-18.734,19.211,-1.76670989022852));
#132378=CARTESIAN_POINT('',(-17.174464231106,17.180864983421,7.14996297786979));
#132379=CARTESIAN_POINT('',(-17.174464231106,17.180864983421,7.08324142508076));
#132380=CARTESIAN_POINT('',(-17.174464231106,17.180864983421,-1.76670989022852));
#132381=CARTESIAN_POINT('',(-21.2939991231355,19.208881145288,6.6332901097715));
#132382=CARTESIAN_POINT('Ctrl Pts',(-21.2939991231355,19.208881145288,6.6332901097715));
#132383=CARTESIAN_POINT('Ctrl Pts',(-21.2940674480299,19.2914312459012,
6.63740642252224));
#132384=CARTESIAN_POINT('Ctrl Pts',(-21.2901386830331,19.374124140816,6.64152273527298));
#132385=CARTESIAN_POINT('Ctrl Pts',(-21.2821979940262,19.4565340775554,
6.64563904802373));
#132386=CARTESIAN_POINT('Ctrl Pts',(-21.2742662779566,19.5388508914942,
6.64975070936244));
#132387=CARTESIAN_POINT('Ctrl Pts',(-21.2623316869624,19.6208849121509,
6.65386237070115));
#132388=CARTESIAN_POINT('Ctrl Pts',(-21.2464314307688,19.7022110602224,
6.65797403203986));
#132389=CARTESIAN_POINT('Ctrl Pts',(-21.2305407999847,19.7834879765415,
6.66208320433541));
#132390=CARTESIAN_POINT('Ctrl Pts',(-21.2106893569246,19.864057405363,6.66619237663095));
#132391=CARTESIAN_POINT('Ctrl Pts',(-21.1869659077107,19.9435013690152,
6.6703015489265));
#132392=CARTESIAN_POINT('Ctrl Pts',(-21.1632492097461,20.0229227244029,
6.67440955182855));
#132393=CARTESIAN_POINT('Ctrl Pts',(-21.1356628286736,20.1012187954781,
6.6785175547306));
#132394=CARTESIAN_POINT('Ctrl Pts',(-21.1043458531985,20.1779852823206,
6.68262555763265));
#132395=CARTESIAN_POINT('Ctrl Pts',(-21.0730277445931,20.2547545467759,
6.68673370917301));
#132396=CARTESIAN_POINT('Ctrl Pts',(-21.0379789552761,20.3299936782021,
6.69084186071338));
#132397=CARTESIAN_POINT('Ctrl Pts',(-20.9993866849092,20.4033184003596,
6.69495001225374));
#132398=CARTESIAN_POINT('Ctrl Pts',(-20.960756173379,20.4767157801412,6.69906223457026));
#132399=CARTESIAN_POINT('Ctrl Pts',(-20.9185753946449,20.5481945435132,
6.70317445688679));
#132400=CARTESIAN_POINT('Ctrl Pts',(-20.8730771242595,20.6173957680787,
6.70728667920331));
#132401=CARTESIAN_POINT('Ctrl Pts',(-20.8275541489316,20.6866345679687,
6.71140113440066));
#132402=CARTESIAN_POINT('Ctrl Pts',(-20.7787103793541,20.7535929860942,
6.71551558959801));
#132403=CARTESIAN_POINT('Ctrl Pts',(-20.7268199445205,20.8179438909686,
6.71963004479536));
#132404=CARTESIAN_POINT('Ctrl Pts',(-20.6748438133911,20.8824010704232,
6.72375129495542));
#132405=CARTESIAN_POINT('Ctrl Pts',(-20.6198112918951,20.9442417891335,
6.72787254511548));
#132406=CARTESIAN_POINT('Ctrl Pts',(-20.5620341095488,21.003175017772,6.73199379527554));
#132407=CARTESIAN_POINT('Ctrl Pts',(-20.5297457003867,21.0361094760174,
6.73429692959298));
#132408=CARTESIAN_POINT('Ctrl Pts',(-20.4966007367166,21.0681366118251,
6.73660006391043));
#132409=CARTESIAN_POINT('Ctrl Pts',(-20.4626578964191,21.0992112903878,
6.73890319822788));
#132410=CARTESIAN_POINT('Ctrl Pts',(-20.400986123379,21.1556718136325,6.74308783262093));
#132411=CARTESIAN_POINT('Ctrl Pts',(-20.3364305466715,21.2092127933027,
6.74727246701397));
#132412=CARTESIAN_POINT('Ctrl Pts',(-20.2692989765722,21.2595255801518,
6.75145710140702));
#132413=CARTESIAN_POINT('Ctrl Pts',(-20.2022629599537,21.3097667529764,
6.75563577949096));
#132414=CARTESIAN_POINT('Ctrl Pts',(-20.1326585979523,21.3567885864285,
6.75981445757491));
#132415=CARTESIAN_POINT('Ctrl Pts',(-20.0608289916761,21.4003206313484,
6.76399313565886));
#132416=CARTESIAN_POINT('Ctrl Pts',(-19.9877118913304,21.4446329568876,
6.76824671354429));
#132417=CARTESIAN_POINT('Ctrl Pts',(-19.9122893426569,21.4853288288423,
6.77250029142973));
#132418=CARTESIAN_POINT('Ctrl Pts',(-19.8349567777299,21.5221672751168,
6.77675386931516));
#132419=CARTESIAN_POINT('Ctrl Pts',(-19.7591234554761,21.5582915362258,
6.78092498329311));
#132420=CARTESIAN_POINT('Ctrl Pts',(-19.6814539493099,21.5907063974351,
6.78509609727106));
#132421=CARTESIAN_POINT('Ctrl Pts',(-19.6023470115176,21.6192303601583,
6.78926721124901));
#132422=CARTESIAN_POINT('Ctrl Pts',(-19.5232666188223,21.6477447513905,
6.79343692556939));
#132423=CARTESIAN_POINT('Ctrl Pts',(-19.4427501848435,21.6723706812233,
6.79760663988976));
#132424=CARTESIAN_POINT('Ctrl Pts',(-19.3612154692016,21.6929751721551,
6.80177635421013));
#132425=CARTESIAN_POINT('Ctrl Pts',(-19.2796836549147,21.7135789298907,
6.80594592015418));
#132426=CARTESIAN_POINT('Ctrl Pts',(-19.1971340772293,21.7301614213603,
6.81011548609822));
#132427=CARTESIAN_POINT('Ctrl Pts',(-19.1139973178553,21.7426401873929,
6.81428505204227));
#132428=CARTESIAN_POINT('Ctrl Pts',(-19.0279375725821,21.755557691445,6.81860121478119));
#132429=CARTESIAN_POINT('Ctrl Pts',(-18.9412491083342,21.7640774486061,
6.82291737752011));
#132430=CARTESIAN_POINT('Ctrl Pts',(-18.8544163259005,21.7681663826307,
6.82723354025903));
#132431=CARTESIAN_POINT('Ctrl Pts',(-18.7704121122214,21.7721221200595,
6.83140910445071));
#132432=CARTESIAN_POINT('Ctrl Pts',(-18.68627330923,21.7719313177434,6.83558466864239));
#132433=CARTESIAN_POINT('Ctrl Pts',(-18.6024375216845,21.7676171622477,
6.83976023283407));
#132434=CARTESIAN_POINT('Ctrl Pts',(-18.5143673878107,21.7630851090138,
6.84414669484661));
#132435=CARTESIAN_POINT('Ctrl Pts',(-18.4266322652435,21.7540022746857,
6.84853315685916));
#132436=CARTESIAN_POINT('Ctrl Pts',(-18.3397299608673,21.7404566879554,
6.8529196188717));
#132437=CARTESIAN_POINT('Ctrl Pts',(-18.252827656491,21.7269111012251,6.85730608088424));
#132438=CARTESIAN_POINT('Ctrl Pts',(-18.1667587226473,21.7089029553708,
6.86169254289678));
#132439=CARTESIAN_POINT('Ctrl Pts',(-18.0820028534405,21.6865806835727,
6.86607900490932));
#132440=CARTESIAN_POINT('Ctrl Pts',(-18.0011467274142,21.6652854925895,
6.87026363930237));
#132441=CARTESIAN_POINT('Ctrl Pts',(-17.9211845272768,21.6399851855304,
6.87444827369542));
#132442=CARTESIAN_POINT('Ctrl Pts',(-17.8425423900639,21.6107715161421,
6.87863290808848));
#132443=CARTESIAN_POINT('Ctrl Pts',(-17.7640121901996,21.5815994287963,
6.88281158617241));
#132444=CARTESIAN_POINT('Ctrl Pts',(-17.6867987486328,21.5485252020904,
6.88699026425635));
#132445=CARTESIAN_POINT('Ctrl Pts',(-17.6113151844297,21.5116909407584,
6.89116894234028));
#132446=CARTESIAN_POINT('Ctrl Pts',(-17.5344786315872,21.4741964517643,
6.89542252022572));
#132447=CARTESIAN_POINT('Ctrl Pts',(-17.4594350484394,21.4328059278378,
6.89967609811115));
#132448=CARTESIAN_POINT('Ctrl Pts',(-17.3866010942662,21.3877214311499,
6.90392967599659));
#132449=CARTESIAN_POINT('Ctrl Pts',(-17.3151791684185,21.3435109854055,
6.90810078997454));
#132450=CARTESIAN_POINT('Ctrl Pts',(-17.2458823693354,21.2957487717616,
6.91227190395249));
#132451=CARTESIAN_POINT('Ctrl Pts',(-17.1790791456549,21.244671836045,6.91644301793044));
#132452=CARTESIAN_POINT('Ctrl Pts',(-17.1122983384412,21.1936120396874,
6.92061273225081));
#132453=CARTESIAN_POINT('Ctrl Pts',(-17.0480098099919,21.139240009464,6.92478244657119));
#132454=CARTESIAN_POINT('Ctrl Pts',(-16.9865514987009,21.0818350369039,
6.92895216089156));
#132455=CARTESIAN_POINT('Ctrl Pts',(-16.9250953743602,21.0244321070591,
6.93312172683561));
#132456=CARTESIAN_POINT('Ctrl Pts',(-16.8664696025459,20.9639967641002,
6.93729129277965));
#132457=CARTESIAN_POINT('Ctrl Pts',(-16.8109765840842,20.9008464255191,
6.9414608587237));
#132458=CARTESIAN_POINT('Ctrl Pts',(-16.7535324995515,20.8354757989379,
6.94577702146262));
#132459=CARTESIAN_POINT('Ctrl Pts',(-16.6994459105392,20.7671961022136,
6.95009318420154));
#132460=CARTESIAN_POINT('Ctrl Pts',(-16.649006825895,20.6963967362073,6.95440934694046));
#132461=CARTESIAN_POINT('Ctrl Pts',(-16.6002107891278,20.6279036521019,
6.95858491113214));
#132462=CARTESIAN_POINT('Ctrl Pts',(-16.5548284854399,20.5570529563656,
6.96276047532382));
#132463=CARTESIAN_POINT('Ctrl Pts',(-16.5130772857549,20.4842251557954,
6.9669360395155));
#132464=CARTESIAN_POINT('Ctrl Pts',(-16.469217332228,20.4077189961501,6.97132250152804));
#132465=CARTESIAN_POINT('Ctrl Pts',(-16.4293652006909,20.3290312765031,
6.97570896354058));
#132466=CARTESIAN_POINT('Ctrl Pts',(-16.3937163263691,20.2486282219257,
6.98009542555312));
#132467=CARTESIAN_POINT('Ctrl Pts',(-16.3580674520474,20.1682251673484,
6.98448188756566));
#132468=CARTESIAN_POINT('Ctrl Pts',(-16.3266219713968,20.0861073468905,
6.98886834957821));
#132469=CARTESIAN_POINT('Ctrl Pts',(-16.2995147249235,20.0027584514457,
6.99325481159075));
#132470=CARTESIAN_POINT('Ctrl Pts',(-16.2736547230431,19.9232445622331,
6.99743944598379));
#132471=CARTESIAN_POINT('Ctrl Pts',(-16.251646255088,19.8423144298573,7.00162408037684));
#132472=CARTESIAN_POINT('Ctrl Pts',(-16.233642830573,19.7603760326905,7.00580871476989));
#132473=CARTESIAN_POINT('Ctrl Pts',(-16.2156650317043,19.6785542646903,
7.00998739285383));
#132474=CARTESIAN_POINT('Ctrl Pts',(-16.2016810508028,19.595727528011,7.01416607093777));
#132475=CARTESIAN_POINT('Ctrl Pts',(-16.1917950137906,19.5123201090072,
7.01834474902171));
#132476=CARTESIAN_POINT('Ctrl Pts',(-16.1817317766699,19.4274176719615,
7.02259832690714));
#132477=CARTESIAN_POINT('Ctrl Pts',(-16.1759149888559,19.3419139888706,
7.02685190479258));
#132478=CARTESIAN_POINT('Ctrl Pts',(-16.1744002778054,19.256268776672,7.03110548267802));
#132479=CARTESIAN_POINT('Ctrl Pts',(-16.1729149323844,19.1722839640347,
7.03527659665598));
#132480=CARTESIAN_POINT('Ctrl Pts',(-16.1755663524988,19.0881635420986,
7.03944771063393));
#132481=CARTESIAN_POINT('Ctrl Pts',(-16.1823546543812,19.0043456262698,
7.04361882461188));
#132482=CARTESIAN_POINT('Ctrl Pts',(-16.1891406783834,18.9205558363522,
7.04778853893226));
#132483=CARTESIAN_POINT('Ctrl Pts',(-16.2000607901197,18.8370688090937,
7.05195825325264));
#132484=CARTESIAN_POINT('Ctrl Pts',(-16.2150630692561,18.7543198724111,
7.05612796757302));
#132485=CARTESIAN_POINT('Ctrl Pts',(-16.230064814547,18.671573880291,7.06029753351705));
#132486=CARTESIAN_POINT('Ctrl Pts',(-16.2491483555177,18.5895663790281,
7.06446709946109));
#132487=CARTESIAN_POINT('Ctrl Pts',(-16.2722104781216,18.5087234519295,
7.06863666540513));
#132488=CARTESIAN_POINT('Ctrl Pts',(-16.2960834365062,18.4250381872445,
7.07295282814405));
#132489=CARTESIAN_POINT('Ctrl Pts',(-16.3242198111559,18.3426014204634,
7.07726899088298));
#132490=CARTESIAN_POINT('Ctrl Pts',(-16.3564491538596,18.2618677784328,
7.0815851536219));
#132491=CARTESIAN_POINT('Ctrl Pts',(-16.3876286291147,18.1837640262997,
7.08576071781358));
#132492=CARTESIAN_POINT('Ctrl Pts',(-16.4226382716204,18.1072545529911,
7.08993628200526));
#132493=CARTESIAN_POINT('Ctrl Pts',(-16.4612757941353,18.0327280941665,
7.09411184619694));
#132494=CARTESIAN_POINT('Ctrl Pts',(-16.5018648060604,17.9544374810766,
7.09849830820948));
#132495=CARTESIAN_POINT('Ctrl Pts',(-16.5464575227364,17.878335974976,7.10288477022202));
#132496=CARTESIAN_POINT('Ctrl Pts',(-16.5947677080407,17.80484026475,7.10727123223456));
#132497=CARTESIAN_POINT('Ctrl Pts',(-16.643077893345,17.7313445545239,7.1116576942471));
#132498=CARTESIAN_POINT('Ctrl Pts',(-16.6951051426578,17.6604550629257,
7.11604415625964));
#132499=CARTESIAN_POINT('Ctrl Pts',(-16.7505157350918,17.592546982189,7.12043061827219));
#132500=CARTESIAN_POINT('Ctrl Pts',(-16.8033793819712,17.5277602935319,
7.1246154567425));
#132501=CARTESIAN_POINT('Ctrl Pts',(-16.8595189473393,17.4654457911716,
7.12880029521283));
#132502=CARTESIAN_POINT('Ctrl Pts',(-16.9186744386476,17.4059534337584,
7.13298513368314));
#132503=CARTESIAN_POINT('Ctrl Pts',(-16.9777385242404,17.3465530025786,
7.13716350583653));
#132504=CARTESIAN_POINT('Ctrl Pts',(-17.0398089529392,17.2899663736295,
7.14134187798991));
#132505=CARTESIAN_POINT('Ctrl Pts',(-17.1045853939259,17.236510688428,7.1455202501433));
#132506=CARTESIAN_POINT('Ctrl Pts',(-17.1275436242151,17.2175647890789,
7.14700115938546));
#132507=CARTESIAN_POINT('Ctrl Pts',(-17.1508414102745,17.1990118720507,
7.14848206862763));
#132508=CARTESIAN_POINT('Ctrl Pts',(-17.174464231106,17.180864983421,7.14996297786979));
#132509=CARTESIAN_POINT('Ctrl Pts',(-17.1721129728022,17.177834880393,6.34984102388608));
#132510=CARTESIAN_POINT('Ctrl Pts',(-17.211840036684,17.1470017875518,6.35235260865192));
#132511=CARTESIAN_POINT('Ctrl Pts',(-17.9391679592174,16.6183204949674,
6.39725612897823));
#132512=CARTESIAN_POINT('Ctrl Pts',(-19.9200693000182,16.4259449961135,
6.48455158486501));
#132513=CARTESIAN_POINT('Ctrl Pts',(-21.2201493011995,18.0710819511262,
6.57652302872765));
#132514=CARTESIAN_POINT('Ctrl Pts',(-21.2969229188781,19.0646440605456,
6.62610253702981));
#132515=CARTESIAN_POINT('Ctrl Pts',(-21.2956375040978,19.2088797892363,
6.6332901097715));
#132516=CARTESIAN_POINT('',(-21.293999428374,19.2127107672549,6.5667098902584));
#132517=CARTESIAN_POINT('Ctrl Pts',(-17.174464231106,17.180864983421,6.28334279855885));
#132518=CARTESIAN_POINT('Ctrl Pts',(-17.2411329207509,17.129650554175,6.28751243593184));
#132519=CARTESIAN_POINT('Ctrl Pts',(-17.3103497458901,17.0817061849628,
6.29168207330483));
#132520=CARTESIAN_POINT('Ctrl Pts',(-17.3817565908666,17.037284801899,6.29585171067782));
#132521=CARTESIAN_POINT('Ctrl Pts',(-17.4531632307407,16.992863546427,6.30002133607433));
#132522=CARTESIAN_POINT('Ctrl Pts',(-17.5267594866646,16.9519654989341,
6.30419096147084));
#132523=CARTESIAN_POINT('Ctrl Pts',(-17.6021597931636,16.914799280074,6.30836058686735));
#132524=CARTESIAN_POINT('Ctrl Pts',(-17.6781541978221,16.8773402191389,
6.31256306580105));
#132525=CARTESIAN_POINT('Ctrl Pts',(-17.7559807895149,16.8436722785943,
6.31676554473475));
#132526=CARTESIAN_POINT('Ctrl Pts',(-17.8352228883562,16.8139602206919,
6.32096802366844));
#132527=CARTESIAN_POINT('Ctrl Pts',(-17.9139613122198,16.784437017203,6.32514379099917));
#132528=CARTESIAN_POINT('Ctrl Pts',(-17.9940968401885,16.758819636878,6.32931955832989));
#132529=CARTESIAN_POINT('Ctrl Pts',(-18.0752057298362,16.7372194702037,
6.33349532566061));
#132530=CARTESIAN_POINT('Ctrl Pts',(-18.1570928770901,16.7154120451871,
6.33771116039579));
#132531=CARTESIAN_POINT('Ctrl Pts',(-18.2399716959823,16.6976994377661,
6.34192699513098));
#132532=CARTESIAN_POINT('Ctrl Pts',(-18.323397753023,16.6841430996637,6.34614282986616));
#132533=CARTESIAN_POINT('Ctrl Pts',(-18.4068238100637,16.6705867615613,
6.35035866460135));
#132534=CARTESIAN_POINT('Ctrl Pts',(-18.4907966255752,16.6611866818601,
6.35457449933654));
#132535=CARTESIAN_POINT('Ctrl Pts',(-18.5748705298082,16.6559505265619,
6.35879033407172));
#132536=CARTESIAN_POINT('Ctrl Pts',(-18.6583222240304,16.650753122744,6.36297496846477));
#132537=CARTESIAN_POINT('Ctrl Pts',(-18.7421841184714,16.6496388297569,
6.36715960285782));
#132538=CARTESIAN_POINT('Ctrl Pts',(-18.8260228331345,16.6526544802975,
6.37134423725088));
#132539=CARTESIAN_POINT('Ctrl Pts',(-18.9097422137643,16.6556658384329,
6.37552291533482));
#132540=CARTESIAN_POINT('Ctrl Pts',(-18.9934380243482,16.6627954472227,
6.37970159341876));
#132541=CARTESIAN_POINT('Ctrl Pts',(-19.0766734176216,16.6740382484445,
6.3838802715027));
#132542=CARTESIAN_POINT('Ctrl Pts',(-19.1614007454992,16.6854825687982,
6.38813384938813));
#132543=CARTESIAN_POINT('Ctrl Pts',(-19.2456505065471,16.7011890198917,
6.39238742727357));
#132544=CARTESIAN_POINT('Ctrl Pts',(-19.328963647833,16.7210967372692,6.396641005159));
#132545=CARTESIAN_POINT('Ctrl Pts',(-19.4106616013028,16.7406185046987,
6.40081211913695));
#132546=CARTESIAN_POINT('Ctrl Pts',(-19.4914584592904,16.7641799807698,
6.4049832331149));
#132547=CARTESIAN_POINT('Ctrl Pts',(-19.5709299408018,16.7916719374609,
6.40915434709286));
#132548=CARTESIAN_POINT('Ctrl Pts',(-19.65037475489,16.8191546689603,6.41332406141323));
#132549=CARTESIAN_POINT('Ctrl Pts',(-19.728494641376,16.8505651114306,6.4174937757336));
#132550=CARTESIAN_POINT('Ctrl Pts',(-19.8048810053294,16.8857443425669,
6.42166349005397));
#132551=CARTESIAN_POINT('Ctrl Pts',(-19.8812646511282,16.9209223218752,
6.42583305599801));
#132552=CARTESIAN_POINT('Ctrl Pts',(-19.9559144795495,16.9598686299933,
6.43000262194205));
#132553=CARTESIAN_POINT('Ctrl Pts',(-20.0284436491278,17.0023769811866,
6.43417218788609));
#132554=CARTESIAN_POINT('Ctrl Pts',(-20.1035228548341,17.046379873568,6.43848835062501));
#132555=CARTESIAN_POINT('Ctrl Pts',(-20.1763290473291,17.0941996856771,
6.44280451336393));
#132556=CARTESIAN_POINT('Ctrl Pts',(-20.2464645244674,17.1455579015069,
6.44712067610285));
#132557=CARTESIAN_POINT('Ctrl Pts',(-20.3143153458149,17.195243128858,6.45129624029454));
#132558=CARTESIAN_POINT('Ctrl Pts',(-20.3796664407518,17.2482394397191,
6.45547180448622));
#132559=CARTESIAN_POINT('Ctrl Pts',(-20.4421918593801,17.3042539310261,
6.4596473686779));
#132560=CARTESIAN_POINT('Ctrl Pts',(-20.5078752882632,17.3630975811272,
6.46403383069044));
#132561=CARTESIAN_POINT('Ctrl Pts',(-20.5704396751019,17.4252719095177,
6.46842029270298));
#132562=CARTESIAN_POINT('Ctrl Pts',(-20.6295529524492,17.490395744379,6.47280675471552));
#132563=CARTESIAN_POINT('Ctrl Pts',(-20.6886662297965,17.5555195792402,
6.47719321672806));
#132564=CARTESIAN_POINT('Ctrl Pts',(-20.7443280892574,17.6235924232491,
6.4815796787406));
#132565=CARTESIAN_POINT('Ctrl Pts',(-20.7962584977302,17.6941974787272,
6.48596614075314));
#132566=CARTESIAN_POINT('Ctrl Pts',(-20.8460908704134,17.7619500256716,
6.4901753857061));
#132567=CARTESIAN_POINT('Ctrl Pts',(-20.8926734978045,17.8322867639503,
6.49438463065905));
#132568=CARTESIAN_POINT('Ctrl Pts',(-20.9357293738867,17.9048653345981,
6.498593875612));
#132569=CARTESIAN_POINT('Ctrl Pts',(-20.9787228581407,17.9773387323842,
6.5027970209913));
#132570=CARTESIAN_POINT('Ctrl Pts',(-21.0181995127222,18.0520471246587,
6.50700016637059));
#132571=CARTESIAN_POINT('Ctrl Pts',(-21.0539239335172,18.1286170073888,
6.51120331174989));
#132572=CARTESIAN_POINT('Ctrl Pts',(-21.0896068791136,18.2050979943154,
6.51540157737787));
#132573=CARTESIAN_POINT('Ctrl Pts',(-21.1215460556625,18.283435770082,6.51959984300585));
#132574=CARTESIAN_POINT('Ctrl Pts',(-21.1495512259746,18.3632310015738,
6.52379810863383));
#132575=CARTESIAN_POINT('Ctrl Pts',(-21.177530608527,18.4429527559101,6.52799250840905));
#132576=CARTESIAN_POINT('Ctrl Pts',(-21.20158303815,18.5241288717761,6.53218690818426));
#132577=CARTESIAN_POINT('Ctrl Pts',(-21.2215663308331,18.6063399717978,
6.53638130795947));
#132578=CARTESIAN_POINT('Ctrl Pts',(-21.2415389226779,18.6885070486596,
6.54057346167871));
#132579=CARTESIAN_POINT('Ctrl Pts',(-21.2574466025638,18.7717075687081,
6.54476561539795));
#132580=CARTESIAN_POINT('Ctrl Pts',(-21.2691973211302,18.8555080269057,
6.54895776911719));
#132581=CARTESIAN_POINT('Ctrl Pts',(-21.2809466969547,18.9392989093157,
6.55314944380356));
#132582=CARTESIAN_POINT('Ctrl Pts',(-21.288539988214,19.0236891460417,6.55734111848993));
#132583=CARTESIAN_POINT('Ctrl Pts',(-21.2919366299884,19.1082371810269,
6.5615327931763));
#132584=CARTESIAN_POINT('Ctrl Pts',(-21.2933350165072,19.1430453357178,
6.56325849219371));
#132585=CARTESIAN_POINT('Ctrl Pts',(-21.294022704555,19.1778801783151,6.56498419121111));
#132586=CARTESIAN_POINT('Ctrl Pts',(-21.2939994283744,19.2127107666517,
6.56670989022851));
#132587=CARTESIAN_POINT('Ctrl Pts',(-21.293999428374,19.2127107672549,6.5667098902584));
#132588=CARTESIAN_POINT('Ctrl Pts',(-21.2939356382109,19.308166639887,6.57143929947813));
#132589=CARTESIAN_POINT('Ctrl Pts',(-21.2885288437516,19.4034153336882,
6.57616870869786));
#132590=CARTESIAN_POINT('Ctrl Pts',(-21.2778724975471,19.4979019278834,
6.5808981179176));
#132591=CARTESIAN_POINT('Ctrl Pts',(-21.2671635859907,19.5928546031339,
6.58565085624617));
#132592=CARTESIAN_POINT('Ctrl Pts',(-21.2511533349013,19.6870374428281,
6.59040359457474));
#132593=CARTESIAN_POINT('Ctrl Pts',(-21.2299860493109,19.7799056526747,
6.59515633290331));
#132594=CARTESIAN_POINT('Ctrl Pts',(-21.2086961910765,19.8733116311444,
6.59993659274384));
#132595=CARTESIAN_POINT('Ctrl Pts',(-21.1821895164634,19.965387517667,6.60471685258437));
#132596=CARTESIAN_POINT('Ctrl Pts',(-21.15066091743,20.055600503295,6.60949711242489));
#132597=CARTESIAN_POINT('Ctrl Pts',(-21.1426476472037,20.0785289255507,
6.61071205742812));
#132598=CARTESIAN_POINT('Ctrl Pts',(-21.134310213157,20.1013371264666,6.61192700243135));
#132599=CARTESIAN_POINT('Ctrl Pts',(-21.1256522921827,20.1240166007786,
6.61314194743458));
#132600=CARTESIAN_POINT('Ctrl Pts',(-21.0958318198279,20.2021315014283,
6.61732658182763));
#132601=CARTESIAN_POINT('Ctrl Pts',(-21.062124806143,20.2789292632222,6.62151121622068));
#132602=CARTESIAN_POINT('Ctrl Pts',(-21.0246680532229,20.3539960060928,
6.62569585061373));
#132603=CARTESIAN_POINT('Ctrl Pts',(-20.9872646153543,20.4289559007464,
6.62987452869768));
#132604=CARTESIAN_POINT('Ctrl Pts',(-20.9461222434274,20.5021892624269,
6.63405320678162));
#132605=CARTESIAN_POINT('Ctrl Pts',(-20.9014264094923,20.5733005393213,
6.63823188486556));
#132606=CARTESIAN_POINT('Ctrl Pts',(-20.8559294348563,20.6456864347473,
6.642485462751));
#132607=CARTESIAN_POINT('Ctrl Pts',(-20.8067505255349,20.715872969927,6.64673904063643));
#132608=CARTESIAN_POINT('Ctrl Pts',(-20.7541351457545,20.7834674854786,
6.65099261852187));
#132609=CARTESIAN_POINT('Ctrl Pts',(-20.7025398177816,20.8497515494465,
6.65516373249982));
#132610=CARTESIAN_POINT('Ctrl Pts',(-20.6476403712487,20.9135428198972,
6.65933484647777));
#132611=CARTESIAN_POINT('Ctrl Pts',(-20.5897118973506,20.9745003130228,
6.66350596045573));
#132612=CARTESIAN_POINT('Ctrl Pts',(-20.5318028619114,21.0354373512728,
6.6676756747761));
#132613=CARTESIAN_POINT('Ctrl Pts',(-20.4708671343699,21.0935421675084,
6.67184538909647));
#132614=CARTESIAN_POINT('Ctrl Pts',(-20.4072185463108,21.1485086312792,
6.67601510341685));
#132615=CARTESIAN_POINT('Ctrl Pts',(-20.3435722231416,21.2034731391074,
6.6801846693609));
#132616=CARTESIAN_POINT('Ctrl Pts',(-20.2772135801198,21.2552992164786,
6.68435423530495));
#132617=CARTESIAN_POINT('Ctrl Pts',(-20.2084905554454,21.3037201441908,
6.68852380124899));
#132618=CARTESIAN_POINT('Ctrl Pts',(-20.1373513140027,21.3538434919877,
6.69283996398791));
#132619=CARTESIAN_POINT('Ctrl Pts',(-20.0636787652558,21.4003174810233,
6.69715612672683));
#132620=CARTESIAN_POINT('Ctrl Pts',(-19.9878910926204,21.4428954114938,
6.70147228946575));
#132621=CARTESIAN_POINT('Ctrl Pts',(-19.9145721954497,21.4840863703576,
6.70564785365743));
#132622=CARTESIAN_POINT('Ctrl Pts',(-19.8392743011541,21.5216310329473,
6.70982341784911));
#132623=CARTESIAN_POINT('Ctrl Pts',(-19.7623989816004,21.555353969571,6.71399898204079));
#132624=CARTESIAN_POINT('Ctrl Pts',(-19.6816408724097,21.5907801715548,
6.71838544405333));
#132625=CARTESIAN_POINT('Ctrl Pts',(-19.5991423447412,21.6219882241026,
6.72277190606586));
#132626=CARTESIAN_POINT('Ctrl Pts',(-19.5153878511232,21.6488336748263,
6.7271583680784));
#132627=CARTESIAN_POINT('Ctrl Pts',(-19.4316333575051,21.67567912555,6.73154483009094));
#132628=CARTESIAN_POINT('Ctrl Pts',(-19.3466234783173,21.6981618996353,
6.73593129210348));
#132629=CARTESIAN_POINT('Ctrl Pts',(-19.2608535512399,21.7161996598167,
6.74031775411602));
#132630=CARTESIAN_POINT('Ctrl Pts',(-19.1790300256489,21.7334074759138,
6.74450238850907));
#132631=CARTESIAN_POINT('Ctrl Pts',(-19.096210294286,21.7466343835296,6.74868702290212));
#132632=CARTESIAN_POINT('Ctrl Pts',(-19.0128164131693,21.755771386146,6.75287165729516));
#132633=CARTESIAN_POINT('Ctrl Pts',(-18.9295412329201,21.7648953833701,
6.75705033537911));
#132634=CARTESIAN_POINT('Ctrl Pts',(-18.8456939795803,21.7699409891981,
6.76122901346306));
#132635=CARTESIAN_POINT('Ctrl Pts',(-18.7617076421301,21.7708500515787,
6.765407691547));
#132636=CARTESIAN_POINT('Ctrl Pts',(-18.6762159099411,21.7717754082492,
6.76966126943244));
#132637=CARTESIAN_POINT('Ctrl Pts',(-18.5905805302511,21.7684143685408,
6.77391484731787));
#132638=CARTESIAN_POINT('Ctrl Pts',(-18.5052645325906,21.7607607899466,
6.77816842520331));
#132639=CARTESIAN_POINT('Ctrl Pts',(-18.4216025520252,21.7532555909081,
6.78233953918126));
#132640=CARTESIAN_POINT('Ctrl Pts',(-18.3382481596057,21.7416228491976,
6.78651065315921));
#132641=CARTESIAN_POINT('Ctrl Pts',(-18.2556369703989,21.7259093049076,
6.79068176713716));
#132642=CARTESIAN_POINT('Ctrl Pts',(-18.1730535021745,21.7102010334492,
6.79485148145753));
#132643=CARTESIAN_POINT('Ctrl Pts',(-18.0912131934262,21.690414764858,6.79902119577791));
#132644=CARTESIAN_POINT('Ctrl Pts',(-18.010543322501,21.6666486792255,6.80319091009828));
#132645=CARTESIAN_POINT('Ctrl Pts',(-17.929876322156,21.6428834392923,6.80736047604232));
#132646=CARTESIAN_POINT('Ctrl Pts',(-17.850380117865,21.6151387947156,6.81153004198637));
#132647=CARTESIAN_POINT('Ctrl Pts',(-17.772467310616,21.5835629364141,6.81569960793041));
#132648=CARTESIAN_POINT('Ctrl Pts',(-17.69181518518,21.5508769098878,6.82001577066933));
#132649=CARTESIAN_POINT('Ctrl Pts',(-17.612860361743,21.5140854441413,6.82433193340825));
#132650=CARTESIAN_POINT('Ctrl Pts',(-17.5360366305503,21.4734066313235,
6.82864809614717));
#132651=CARTESIAN_POINT('Ctrl Pts',(-17.4617154243207,21.4340529265546,
6.83282366033885));
#132652=CARTESIAN_POINT('Ctrl Pts',(-17.3893889826097,21.3910615273711,
6.83699922453053));
#132653=CARTESIAN_POINT('Ctrl Pts',(-17.3194221772609,21.3446751353978,
6.84117478872221));
#132654=CARTESIAN_POINT('Ctrl Pts',(-17.2459215149042,21.295945877039,6.84556125073475));
#132655=CARTESIAN_POINT('Ctrl Pts',(-17.1750255931743,21.2434699978814,
6.84994771274729));
#132656=CARTESIAN_POINT('Ctrl Pts',(-17.1071180986345,21.1875766564971,
6.85433417475983));
#132657=CARTESIAN_POINT('Ctrl Pts',(-17.0392106040947,21.1316833151128,
6.85872063677237));
#132658=CARTESIAN_POINT('Ctrl Pts',(-16.9742919138006,21.0723729590137,
6.86310709878491));
#132659=CARTESIAN_POINT('Ctrl Pts',(-16.9126993772538,21.0100175211999,
6.86749356079745));
#132660=CARTESIAN_POINT('Ctrl Pts',(-16.8539408046156,20.9505311495128,
6.8716781951905));
#132661=CARTESIAN_POINT('Ctrl Pts',(-16.7979903187279,20.8880523361676,
6.87586282958355));
#132662=CARTESIAN_POINT('Ctrl Pts',(-16.7451680193311,20.8228769657355,
6.8800474639766));
#132663=CARTESIAN_POINT('Ctrl Pts',(-16.6924209059394,20.7577943643761,
6.88422614206054));
#132664=CARTESIAN_POINT('Ctrl Pts',(-16.6427934219786,20.6900231841701,
6.88840482014448));
#132665=CARTESIAN_POINT('Ctrl Pts',(-16.5965688328438,20.6198960237254,
6.89258349822842));
#132666=CARTESIAN_POINT('Ctrl Pts',(-16.5495157011699,20.5485118843294,
6.89683707611386));
#132667=CARTESIAN_POINT('Ctrl Pts',(-16.5059889968458,20.4746868150557,
6.9010906539993));
#132668=CARTESIAN_POINT('Ctrl Pts',(-16.4662445138507,20.3988068256411,
6.90534423188473));
#132669=CARTESIAN_POINT('Ctrl Pts',(-16.4272705552135,20.324397917889,6.90951534586268));
#132670=CARTESIAN_POINT('Ctrl Pts',(-16.3919336983952,20.2480134825273,
6.91368645984064));
#132671=CARTESIAN_POINT('Ctrl Pts',(-16.3604304325482,20.1700451024153,
6.91785757381859));
#132672=CARTESIAN_POINT('Ctrl Pts',(-16.3289377379264,20.0921028853462,
6.92202728813896));
#132673=CARTESIAN_POINT('Ctrl Pts',(-16.3012762516654,20.0125782052864,
6.92619700245933));
#132674=CARTESIAN_POINT('Ctrl Pts',(-16.2775946975111,19.9318834787288,
6.9303667167797));
#132675=CARTESIAN_POINT('Ctrl Pts',(-16.253913986048,19.8511916236358,6.93453628272375));
#132676=CARTESIAN_POINT('Ctrl Pts',(-16.2342130538339,19.7693302464836,
6.93870584866779));
#132677=CARTESIAN_POINT('Ctrl Pts',(-16.2185906288469,19.6867264923412,
6.94287541461184));
#132678=CARTESIAN_POINT('Ctrl Pts',(-16.2024189386698,19.6012184921059,
6.94719157735076));
#132679=CARTESIAN_POINT('Ctrl Pts',(-16.1906179905571,19.5149154578638,
6.95150774008967));
#132680=CARTESIAN_POINT('Ctrl Pts',(-16.1832392059578,19.4283001877062,
6.95582390282859));
#132681=CARTESIAN_POINT('Ctrl Pts',(-16.1761007844908,19.3445064008637,
6.95999946702027));
#132682=CARTESIAN_POINT('Ctrl Pts',(-16.1731008165489,19.2604208803106,
6.96417503121195));
#132683=CARTESIAN_POINT('Ctrl Pts',(-16.1742327266829,19.1764817953116,
6.96835059540363));
#132684=CARTESIAN_POINT('Ctrl Pts',(-16.175421806907,19.0883031466756,6.97273705741617));
#132685=CARTESIAN_POINT('Ctrl Pts',(-16.1811710990057,19.0002866979193,
6.97712351942872));
#132686=CARTESIAN_POINT('Ctrl Pts',(-16.1914115149699,18.912933236015,6.98150998144126));
#132687=CARTESIAN_POINT('Ctrl Pts',(-16.2016519309342,18.8255797741108,
6.9858964434538));
#132688=CARTESIAN_POINT('Ctrl Pts',(-16.2163832985703,18.7388898583324,
6.99028290546634));
#132689=CARTESIAN_POINT('Ctrl Pts',(-16.2354754819718,18.6533484665025,
6.99466936747888));
#132690=CARTESIAN_POINT('Ctrl Pts',(-16.2536851821496,18.571760988253,6.99885307745115));
#132691=CARTESIAN_POINT('Ctrl Pts',(-16.2759292313583,18.4909145868875,
7.00303678742343));
#132692=CARTESIAN_POINT('Ctrl Pts',(-16.3021321571691,18.4112382886104,
7.0072204973957));
#132693=CARTESIAN_POINT('Ctrl Pts',(-16.3283004575787,18.3316672771937,
7.0113986788771));
#132694=CARTESIAN_POINT('Ctrl Pts',(-16.3584171062891,18.2532637320032,
7.01557686035851));
#132695=CARTESIAN_POINT('Ctrl Pts',(-16.3923558259029,18.1764457182356,
7.01975504183991));
#132696=CARTESIAN_POINT('Ctrl Pts',(-16.426259882933,18.0997061608994,7.02392895602523));
#132697=CARTESIAN_POINT('Ctrl Pts',(-16.4639780734706,18.0245493373741,
7.02810287021055));
#132698=CARTESIAN_POINT('Ctrl Pts',(-16.5053350197041,17.95137608565,7.03227678439588));
#132699=CARTESIAN_POINT('Ctrl Pts',(-16.5474166608013,17.8769206241758,
7.03652383778628));
#132700=CARTESIAN_POINT('Ctrl Pts',(-16.5932656413836,17.8045193749155,
7.04077089117669));
#132701=CARTESIAN_POINT('Ctrl Pts',(-16.642647159626,17.734570761242,7.0450179445671));
#132702=CARTESIAN_POINT('Ctrl Pts',(-16.6911293348285,17.6658960613949,
7.04918765003378));
#132703=CARTESIAN_POINT('Ctrl Pts',(-16.7430161596747,17.5995857851865,
7.05335735550045));
#132704=CARTESIAN_POINT('Ctrl Pts',(-16.7980414116622,17.5359882554916,
7.05752706096713));
#132705=CARTESIAN_POINT('Ctrl Pts',(-16.8545977390559,17.4706211271108,
7.0618127883194));
#132706=CARTESIAN_POINT('Ctrl Pts',(-16.9144694416338,17.4081203624224,
7.06609851567167));
#132707=CARTESIAN_POINT('Ctrl Pts',(-16.9773240231389,17.3488266696359,
7.07038424302394));
#132708=CARTESIAN_POINT('Ctrl Pts',(-17.040178604644,17.2895329768495,7.07466997037622));
#132709=CARTESIAN_POINT('Ctrl Pts',(-17.1060156660477,17.2334467007285,
7.07895569772849));
#132710=CARTESIAN_POINT('Ctrl Pts',(-17.174464231106,17.180864983421,7.08324142508076));
#132711=CARTESIAN_POINT('Origin',(-18.734,19.211,-1.76670989022852));
#132712=CARTESIAN_POINT('',(-17.1770150831773,17.1841768308936,7.94987222090926));
#132713=CARTESIAN_POINT('',(-17.171894433269,17.1775280041638,7.88329696157113));
#132714=CARTESIAN_POINT('',(-17.174464231106,17.180864983421,-1.76670989022852));
#132715=CARTESIAN_POINT('',(-21.2936354886768,19.2104398261304,7.43329008494697));
#132716=CARTESIAN_POINT('Ctrl Pts',(-21.2898971261407,19.2104411453458,
7.4332901097715));
#132717=CARTESIAN_POINT('Ctrl Pts',(-21.2889976171803,19.6723917155128,
7.45617941928649));
#132718=CARTESIAN_POINT('Ctrl Pts',(-20.9482576239576,20.9911305382399,
7.52146066436197));
#132719=CARTESIAN_POINT('Ctrl Pts',(-18.8327965349617,22.2364802930772,
7.62913384499793));
#132720=CARTESIAN_POINT('Ctrl Pts',(-16.2435265567091,20.9317073508827,
7.75630965167935));
#132721=CARTESIAN_POINT('Ctrl Pts',(-15.9876140791817,18.5077088656147,
7.8632224436498));
#132722=CARTESIAN_POINT('Ctrl Pts',(-16.82314712442,17.4566899468327,7.92774330005977));
#132723=CARTESIAN_POINT('Ctrl Pts',(-17.1770150831773,17.1841768308936,
7.94987222090926));
#132724=CARTESIAN_POINT('Ctrl Pts',(-17.174464231106,17.180864983421,7.14996297786979));
#132725=CARTESIAN_POINT('Ctrl Pts',(-17.2410259123316,17.1297327573074,
7.15413571446225));
#132726=CARTESIAN_POINT('Ctrl Pts',(-17.3101705590919,17.0818270774072,
7.1583084510547));
#132727=CARTESIAN_POINT('Ctrl Pts',(-17.381550029553,17.0374133149474,7.16248118764716));
#132728=CARTESIAN_POINT('Ctrl Pts',(-17.4528913210709,16.9930233082048,
7.16665169235597));
#132729=CARTESIAN_POINT('Ctrl Pts',(-17.5264646731537,16.9521217531168,
7.17082219706478));
#132730=CARTESIAN_POINT('Ctrl Pts',(-17.6018924712092,16.9149310673991,
7.17499270177359));
#132731=CARTESIAN_POINT('Ctrl Pts',(-17.6773025517232,16.8777491175523,
7.17916222685563));
#132732=CARTESIAN_POINT('Ctrl Pts',(-17.7545658004615,16.8442765088668,
7.18333175193767));
#132733=CARTESIAN_POINT('Ctrl Pts',(-17.833280695483,16.8146893493392,7.18750127701971));
#132734=CARTESIAN_POINT('Ctrl Pts',(-17.9120007132346,16.7851002642925,
7.19167107345258));
#132735=CARTESIAN_POINT('Ctrl Pts',(-17.9921721337704,16.7593972911318,
7.19584086988545));
#132736=CARTESIAN_POINT('Ctrl Pts',(-18.0733754774907,16.7377076112478,
7.20001066631832));
#132737=CARTESIAN_POINT('Ctrl Pts',(-18.1546632779953,16.7159953726794,
7.20418479961198));
#132738=CARTESIAN_POINT('Ctrl Pts',(-18.2369846995719,16.698304881881,7.20835893290564));
#132739=CARTESIAN_POINT('Ctrl Pts',(-18.3199076637616,16.6847126970456,
7.2125330661993));
#132740=CARTESIAN_POINT('Ctrl Pts',(-18.4028746699408,16.671113293138,7.21670941645586));
#132741=CARTESIAN_POINT('Ctrl Pts',(-18.4864433975924,16.6616165818563,
7.22088576671241));
#132742=CARTESIAN_POINT('Ctrl Pts',(-18.570176627374,16.6562471934488,7.22506211696897));
#132743=CARTESIAN_POINT('Ctrl Pts',(-18.6540564596485,16.650868404165,7.22924577929698));
#132744=CARTESIAN_POINT('Ctrl Pts',(-18.7381009088209,16.6496313792551,
7.23342944162499));
#132745=CARTESIAN_POINT('Ctrl Pts',(-18.8218729238928,16.6525085794073,
7.23761310395301));
#132746=CARTESIAN_POINT('Ctrl Pts',(-18.8885737051579,16.6547994577853,
7.24094421095321));
#132747=CARTESIAN_POINT('Ctrl Pts',(-18.9551017385725,16.6596975633221,
7.24427531795342));
#132748=CARTESIAN_POINT('Ctrl Pts',(-19.0212404493958,16.6671657042506,
7.24760642495362));
#132749=CARTESIAN_POINT('Ctrl Pts',(-19.1043258393295,16.6765474021004,
7.25179105934667));
#132750=CARTESIAN_POINT('Ctrl Pts',(-19.1871057341706,16.6900213769478,
7.25597569373972));
#132751=CARTESIAN_POINT('Ctrl Pts',(-19.2691452086513,16.7075584477249,
7.26016032813276));
#132752=CARTESIAN_POINT('Ctrl Pts',(-19.3510679100948,16.7250705566525,
7.26433900621671));
#132753=CARTESIAN_POINT('Ctrl Pts',(-19.4322518385269,16.7466341786848,
7.26851768430066));
#132754=CARTESIAN_POINT('Ctrl Pts',(-19.5122676703941,16.7721684286898,
7.27269636238461));
#132755=CARTESIAN_POINT('Ctrl Pts',(-19.5937177285411,16.798160361775,7.27694994027005));
#132756=CARTESIAN_POINT('Ctrl Pts',(-19.6739569228737,16.8282666158666,
7.28120351815548));
#132757=CARTESIAN_POINT('Ctrl Pts',(-19.7525437584805,16.8623474901424,
7.28545709604092));
#132758=CARTESIAN_POINT('Ctrl Pts',(-19.8296070349296,16.8957676401671,
7.28962821001887));
#132759=CARTESIAN_POINT('Ctrl Pts',(-19.9050810078235,16.9330094826423,
7.29379932399683));
#132760=CARTESIAN_POINT('Ctrl Pts',(-19.9785668286283,16.9738917305866,
7.29797043797478));
#132761=CARTESIAN_POINT('Ctrl Pts',(-20.0520279905562,17.0147602600976,
7.30214015229516));
#132762=CARTESIAN_POINT('Ctrl Pts',(-20.1235019236784,17.0592665455509,
7.30630986661553));
#132763=CARTESIAN_POINT('Ctrl Pts',(-20.1926138614937,17.1071830870871,
7.31047958093591));
#132764=CARTESIAN_POINT('Ctrl Pts',(-20.2617233400095,17.155097923547,7.31464914687994));
#132765=CARTESIAN_POINT('Ctrl Pts',(-20.3284706127603,17.2064225119979,
7.31881871282398));
#132766=CARTESIAN_POINT('Ctrl Pts',(-20.3925105653945,17.2608864893358,
7.32298827876801));
#132767=CARTESIAN_POINT('Ctrl Pts',(-20.4588020837616,17.3172653529285,
7.32730444150693));
#132768=CARTESIAN_POINT('Ctrl Pts',(-20.5221919593123,17.3770081330231,
7.33162060424585));
#132769=CARTESIAN_POINT('Ctrl Pts',(-20.582336932496,17.4397714478444,7.33593676698477));
#132770=CARTESIAN_POINT('Ctrl Pts',(-20.6405226895044,17.500490254287,7.34011233117645));
#132771=CARTESIAN_POINT('Ctrl Pts',(-20.6956714299403,17.5640354429536,
7.34428789536813));
#132772=CARTESIAN_POINT('Ctrl Pts',(-20.7475130548915,17.6300619310734,
7.34846345955981));
#132773=CARTESIAN_POINT('Ctrl Pts',(-20.8019730770773,17.699423260145,7.35284992157235));
#132774=CARTESIAN_POINT('Ctrl Pts',(-20.8527827827184,17.771522659754,7.35723638358489));
#132775=CARTESIAN_POINT('Ctrl Pts',(-20.8996813854342,17.8459270580721,
7.36162284559743));
#132776=CARTESIAN_POINT('Ctrl Pts',(-20.94657998815,17.9203314563902,7.36600930760997));
#132777=CARTESIAN_POINT('Ctrl Pts',(-20.9895672706481,17.9970403100744,
7.37039576962251));
#132778=CARTESIAN_POINT('Ctrl Pts',(-21.0284398795321,18.0755945044995,
7.37478223163505));
#132779=CARTESIAN_POINT('Ctrl Pts',(-21.0682036058612,18.1559494788324,
7.37926924910127));
#132780=CARTESIAN_POINT('Ctrl Pts',(-21.103794382086,18.2385006465155,7.38375626656748));
#132781=CARTESIAN_POINT('Ctrl Pts',(-21.1349820909848,18.3228080169409,
7.3882432840337));
#132782=CARTESIAN_POINT('Ctrl Pts',(-21.1660643193882,18.4068302499356,
7.39271512587973));
#132783=CARTESIAN_POINT('Ctrl Pts',(-21.1927730322953,18.4925965155768,
7.39718696772576));
#132784=CARTESIAN_POINT('Ctrl Pts',(-21.214925712994,18.5796462112212,7.40165880957179));
#132785=CARTESIAN_POINT('Ctrl Pts',(-21.2370311427379,18.6665102326671,
7.40612111312312));
#132786=CARTESIAN_POINT('Ctrl Pts',(-21.2545997969947,18.7546518909174,
7.41058341667445));
#132787=CARTESIAN_POINT('Ctrl Pts',(-21.2674980351242,18.8435932689487,
7.41504572022578));
#132788=CARTESIAN_POINT('Ctrl Pts',(-21.2803582069864,18.9322721563795,
7.41949485428542));
#132789=CARTESIAN_POINT('Ctrl Pts',(-21.2885753721633,19.0217457093728,
7.42394398834505));
#132790=CARTESIAN_POINT('Ctrl Pts',(-21.292066600817,19.1115250494615,7.42839312240469));
#132791=CARTESIAN_POINT('Ctrl Pts',(-21.2933474798424,19.1444637323838,
7.43002544244541));
#132792=CARTESIAN_POINT('Ctrl Pts',(-21.2939927168566,19.1774434535922,
7.43165776248613));
#132793=CARTESIAN_POINT('Ctrl Pts',(-21.2939999386838,19.2104396975212,
7.43329008252684));
#132794=CARTESIAN_POINT('',(-21.2941234764334,19.2121301833364,7.36670989022851));
#132795=CARTESIAN_POINT('Ctrl Pts',(-17.174464231106,17.180864983421,7.08324142508076));
#132796=CARTESIAN_POINT('Ctrl Pts',(-17.2411541047993,17.1296342807345,
7.08741703658648));
#132797=CARTESIAN_POINT('Ctrl Pts',(-17.3103224735721,17.0817304249996,
7.09159264809219));
#132798=CARTESIAN_POINT('Ctrl Pts',(-17.3815968316152,17.0373841944486,
7.09576825959791));
#132799=CARTESIAN_POINT('Ctrl Pts',(-17.4557821871669,16.9912267688173,
7.10011441202498));
#132800=CARTESIAN_POINT('Ctrl Pts',(-17.5322487591342,16.9489240726657,
7.10446056445205));
#132801=CARTESIAN_POINT('Ctrl Pts',(-17.6105502686896,16.9106824781743,
7.10880671687912));
#132802=CARTESIAN_POINT('Ctrl Pts',(-17.688851778245,16.8724408836828,7.11315286930619));
#132803=CARTESIAN_POINT('Ctrl Pts',(-17.7689876871541,16.8382605409109,
7.11749902173325));
#132804=CARTESIAN_POINT('Ctrl Pts',(-17.8504927560597,16.8082900820313,
7.12184517416032));
#132805=CARTESIAN_POINT('Ctrl Pts',(-17.9289688151197,16.7794334289094,
7.12602980855337));
#132806=CARTESIAN_POINT('Ctrl Pts',(-18.0090061529611,16.7543718340009,
7.13021444294642));
#132807=CARTESIAN_POINT('Ctrl Pts',(-18.0902029058994,16.733274167381,7.13439907733947));
#132808=CARTESIAN_POINT('Ctrl Pts',(-18.17128408531,16.7122065306782,7.13857775542341));
#132809=CARTESIAN_POINT('Ctrl Pts',(-18.2535209603945,16.6950917298573,
7.14275643350736));
#132810=CARTESIAN_POINT('Ctrl Pts',(-18.3364934985375,16.6820499053372,
7.1469351115913));
#132811=CARTESIAN_POINT('Ctrl Pts',(-18.4209532597953,16.6687743154856,
7.15118868947673));
#132812=CARTESIAN_POINT('Ctrl Pts',(-18.5061748645252,16.6597193207395,
7.15544226736217));
#132813=CARTESIAN_POINT('Ctrl Pts',(-18.5917010358989,16.654957941501,7.1596958452476));
#132814=CARTESIAN_POINT('Ctrl Pts',(-18.6755691155499,16.6502888708901,
7.16386695922556));
#132815=CARTESIAN_POINT('Ctrl Pts',(-18.7597295775162,16.6497484479464,
7.16803807320351));
#132816=CARTESIAN_POINT('Ctrl Pts',(-18.8437446259188,16.6533534026215,
7.17220918718146));
#132817=CARTESIAN_POINT('Ctrl Pts',(-18.9277314822606,16.6569571476192,
7.17637890150183));
#132818=CARTESIAN_POINT('Ctrl Pts',(-19.0115725627189,16.6647034879404,
7.18054861582221));
#132819=CARTESIAN_POINT('Ctrl Pts',(-19.0948308836175,16.6765570486934,
7.18471833014258));
#132820=CARTESIAN_POINT('Ctrl Pts',(-19.1780862418277,16.6884101876458,
7.18888789608662));
#132821=CARTESIAN_POINT('Ctrl Pts',(-19.2607584263887,16.7043701907563,
7.19305746203066));
#132822=CARTESIAN_POINT('Ctrl Pts',(-19.3424177464726,16.7243500757491,
7.19722702797471));
#132823=CARTESIAN_POINT('Ctrl Pts',(-19.426948107513,16.7450324288504,7.20154319071363));
#132824=CARTESIAN_POINT('Ctrl Pts',(-19.5103925419324,16.7700224760727,
7.20585935345255));
#132825=CARTESIAN_POINT('Ctrl Pts',(-19.5922902863025,16.799167131736,7.21017551619147));
#132826=CARTESIAN_POINT('Ctrl Pts',(-19.6715202202638,16.8273624033065,
7.21435108038315));
#132827=CARTESIAN_POINT('Ctrl Pts',(-19.7493022661266,16.8594455439839,
7.21852664457483));
#132828=CARTESIAN_POINT('Ctrl Pts',(-19.8252402968867,16.8952291532946,
7.22270220876651));
#132829=CARTESIAN_POINT('Ctrl Pts',(-19.9050137770549,16.9328201076441,
7.22708867077905));
#132830=CARTESIAN_POINT('Ctrl Pts',(-19.982751549524,16.9744949002993,7.23147513279159));
#132831=CARTESIAN_POINT('Ctrl Pts',(-20.0580263707389,17.0199833023028,
7.23586159480413));
#132832=CARTESIAN_POINT('Ctrl Pts',(-20.1333011919539,17.0654717043063,
7.24024805681667));
#132833=CARTESIAN_POINT('Ctrl Pts',(-20.2061126241217,17.1147733273606,
7.24463451882921));
#132834=CARTESIAN_POINT('Ctrl Pts',(-20.2760730898188,17.1675689183003,
7.24902098084175));
#132835=CARTESIAN_POINT('Ctrl Pts',(-20.3421228419793,17.2174132934338,
7.25316224442401));
#132836=CARTESIAN_POINT('Ctrl Pts',(-20.4058887674611,17.270565700162,7.25730350800627));
#132837=CARTESIAN_POINT('Ctrl Pts',(-20.4670153688585,17.3267872383141,
7.26144477158854));
#132838=CARTESIAN_POINT('Ctrl Pts',(-20.5280546973635,17.3829285067286,
7.26558012252323));
#132839=CARTESIAN_POINT('Ctrl Pts',(-20.5864618395734,17.4421298917808,
7.26971547345792));
#132840=CARTESIAN_POINT('Ctrl Pts',(-20.6419120481561,17.5041105435615,
7.27385082439261));
#132841=CARTESIAN_POINT('Ctrl Pts',(-20.6972986881793,17.5660201402308,
7.27798143452815));
#132842=CARTESIAN_POINT('Ctrl Pts',(-20.7497348173451,17.6307023247237,
7.28211204466368));
#132843=CARTESIAN_POINT('Ctrl Pts',(-20.7989315869956,17.6978385608179,
7.28624265479922));
#132844=CARTESIAN_POINT('Ctrl Pts',(-20.8480980593209,17.7649334517507,
7.29037072114094));
#132845=CARTESIAN_POINT('Ctrl Pts',(-20.8940288533085,17.8344790168689,
7.29449878748265));
#132846=CARTESIAN_POINT('Ctrl Pts',(-20.9364753744698,17.9061236744987,
7.29862685382437));
#132847=CARTESIAN_POINT('Ctrl Pts',(-20.9789091334294,17.9777467910562,
7.30275367899922));
#132848=CARTESIAN_POINT('Ctrl Pts',(-21.0178604599825,18.0514673424199,
7.30688050417407));
#132849=CARTESIAN_POINT('Ctrl Pts',(-21.0531249145872,18.1269060785426,
7.31100732934892));
#132850=CARTESIAN_POINT('Ctrl Pts',(-21.0883898804923,18.2023459084539,
7.31513421435873));
#132851=CARTESIAN_POINT('Ctrl Pts',(-21.1199676712092,18.2795035453347,
7.31926109936855));
#132852=CARTESIAN_POINT('Ctrl Pts',(-21.147701166054,18.3579779129534,7.32338798437837));
#132853=CARTESIAN_POINT('Ctrl Pts',(-21.175460263615,18.4365247257135,7.32751867920249));
#132854=CARTESIAN_POINT('Ctrl Pts',(-21.1993678247307,18.5163902510463,
7.33164937402661));
#132855=CARTESIAN_POINT('Ctrl Pts',(-21.2193162430201,18.5971570459961,
7.33578006885072));
#132856=CARTESIAN_POINT('Ctrl Pts',(-21.2392749611598,18.6779655427927,
7.33991289645234));
#132857=CARTESIAN_POINT('Ctrl Pts',(-21.2552703785523,18.7596757735081,
7.34404572405396));
#132858=CARTESIAN_POINT('Ctrl Pts',(-21.267246258349,18.8418612800574,7.34817855165558));
#132859=CARTESIAN_POINT('Ctrl Pts',(-21.2792406903518,18.9241741027191,
7.35231778154839));
#132860=CARTESIAN_POINT('Ctrl Pts',(-21.2872031132021,19.0069632027568,
7.35645701144119));
#132861=CARTESIAN_POINT('Ctrl Pts',(-21.291129302603,19.0897988045891,7.360596241334));
#132862=CARTESIAN_POINT('Ctrl Pts',(-21.2930622985235,19.1305815748695,
7.36263412429883));
#132863=CARTESIAN_POINT('Ctrl Pts',(-21.2940177418851,19.1713756409973,
7.36467200726367));
#132864=CARTESIAN_POINT('Ctrl Pts',(-21.2939997505486,19.2121301287168,
7.36670989022851));
#132865=CARTESIAN_POINT('Ctrl Pts',(-21.2976211331247,19.2121317273999,
7.36670989022851));
#132866=CARTESIAN_POINT('Ctrl Pts',(-21.2979709119767,19.2754624155768,
7.36987218932674));
#132867=CARTESIAN_POINT('Ctrl Pts',(-21.2671018166522,20.1874206516717,
7.41542642398545));
#132868=CARTESIAN_POINT('Ctrl Pts',(-20.178486706887,21.871216118483,7.50337259420462));
#132869=CARTESIAN_POINT('Ctrl Pts',(-17.2790524902644,21.8655092554602,
7.63054840088606));
#132870=CARTESIAN_POINT('Ctrl Pts',(-15.7210162867422,19.4347114151187,
7.75718985667495));
#132871=CARTESIAN_POINT('Ctrl Pts',(-16.5081485987195,17.6886843918709,
7.84143937690338));
#132872=CARTESIAN_POINT('Ctrl Pts',(-17.171894433272,17.1775280041615,7.88329696157133));
#132873=CARTESIAN_POINT('Origin',(-18.734,19.211,-1.76670989022852));
#132874=CARTESIAN_POINT('',(-17.174464231106,17.180864983421,8.74981199461744));
#132875=CARTESIAN_POINT('',(-17.174464231106,17.180864983421,8.68337762993461));
#132876=CARTESIAN_POINT('',(-17.174464231106,17.180864983421,-1.76670989022852));
#132877=CARTESIAN_POINT('',(-21.2939989173812,19.2133543591349,8.2332901225083));
#132878=CARTESIAN_POINT('Ctrl Pts',(-21.2939989173812,19.2133543591349,
8.2332901225083));
#132879=CARTESIAN_POINT('Ctrl Pts',(-21.2938985191577,19.3225217922602,
8.2387181286671));
#132880=CARTESIAN_POINT('Ctrl Pts',(-21.2868114603045,19.4313771443117,
8.2441461348259));
#132881=CARTESIAN_POINT('Ctrl Pts',(-21.2728791636074,19.5391654957492,
8.2495741409847));
#132882=CARTESIAN_POINT('Ctrl Pts',(-21.2596700733155,19.6413587017587,
8.2547203867915));
#132883=CARTESIAN_POINT('Ctrl Pts',(-21.2403084403105,19.7425933354651,
8.2598666325983));
#132884=CARTESIAN_POINT('Ctrl Pts',(-21.2149532278239,19.84224565848,8.26501287840509));
#132885=CARTESIAN_POINT('Ctrl Pts',(-21.1943358111288,19.9232772597465,
8.26919751279814));
#132886=CARTESIAN_POINT('Ctrl Pts',(-21.1697059337058,20.0034485022604,
8.27338214719119));
#132887=CARTESIAN_POINT('Ctrl Pts',(-21.1411517779373,20.0823324956486,
8.27756678158424));
#132888=CARTESIAN_POINT('Ctrl Pts',(-21.1126382654752,20.1611042074361,
8.28174545966818));
#132889=CARTESIAN_POINT('Ctrl Pts',(-21.0802117249137,20.2385918806366,
8.28592413775212));
#132890=CARTESIAN_POINT('Ctrl Pts',(-21.04401079686,20.3143812207891,8.29010281583607));
#132891=CARTESIAN_POINT('Ctrl Pts',(-21.0071609931882,20.391529030395,8.2943563937215));
#132892=CARTESIAN_POINT('Ctrl Pts',(-20.9664002781982,20.466916555597,8.29860997160694));
#132893=CARTESIAN_POINT('Ctrl Pts',(-20.9219272181894,20.5401254598066,
8.30286354949238));
#132894=CARTESIAN_POINT('Ctrl Pts',(-20.8783163552309,20.6119150665525,
8.30703466347033));
#132895=CARTESIAN_POINT('Ctrl Pts',(-20.8311360546878,20.6816093608382,
8.31120577744828));
#132896=CARTESIAN_POINT('Ctrl Pts',(-20.7806202689677,20.7488379221005,
8.31537689142623));
#132897=CARTESIAN_POINT('Ctrl Pts',(-20.7301214343075,20.8160439241698,
8.3195466057466));
#132898=CARTESIAN_POINT('Ctrl Pts',(-20.6762896134471,20.880785468974,8.32371632006697));
#132899=CARTESIAN_POINT('Ctrl Pts',(-20.6194012584855,20.9427222913912,
8.32788603438734));
#132900=CARTESIAN_POINT('Ctrl Pts',(-20.5625149278558,21.0046569098304,
8.33205560033138));
#132901=CARTESIAN_POINT('Ctrl Pts',(-20.5025725911955,21.0637866660878,
8.33622516627542));
#132902=CARTESIAN_POINT('Ctrl Pts',(-20.4398891227943,21.1198065121253,
8.34039473221946));
#132903=CARTESIAN_POINT('Ctrl Pts',(-20.3750017809724,21.1777959468417,
8.34471089495838));
#132904=CARTESIAN_POINT('Ctrl Pts',(-20.3071773578721,21.2324523620815,
8.3490270576973));
#132905=CARTESIAN_POINT('Ctrl Pts',(-20.2368028123899,21.2834824986168,
8.35334322043622));
#132906=CARTESIAN_POINT('Ctrl Pts',(-20.1687207103247,21.3328503338218,
8.3575187846279));
#132907=CARTESIAN_POINT('Ctrl Pts',(-20.0982524952706,21.3788242964684,
8.36169434881958));
#132908=CARTESIAN_POINT('Ctrl Pts',(-20.0257768405867,21.4211838371782,
8.36586991301126));
#132909=CARTESIAN_POINT('Ctrl Pts',(-19.949640612879,21.4656828575891,8.37025637502381));
#132910=CARTESIAN_POINT('Ctrl Pts',(-19.8712893431909,21.5061924632349,
8.37464283703635));
#132911=CARTESIAN_POINT('Ctrl Pts',(-19.7911876038236,21.5425133219267,
8.3790292990489));
#132912=CARTESIAN_POINT('Ctrl Pts',(-19.7110858644562,21.5788341806186,
8.38341576106144));
#132913=CARTESIAN_POINT('Ctrl Pts',(-19.6292342232969,21.6109661511407,
8.38780222307398));
#132914=CARTESIAN_POINT('Ctrl Pts',(-19.5461152252309,21.638770347654,8.39218868508653));
#132915=CARTESIAN_POINT('Ctrl Pts',(-19.4668206554779,21.66529523187,8.39637331947957));
#132916=CARTESIAN_POINT('Ctrl Pts',(-19.3860776423915,21.6879805757247,
8.40055795387262));
#132917=CARTESIAN_POINT('Ctrl Pts',(-19.3042928646695,21.7066694589843,
8.40474258826567));
#132918=CARTESIAN_POINT('Ctrl Pts',(-19.2226244974556,21.7253317409318,
8.40892126634962));
#132919=CARTESIAN_POINT('Ctrl Pts',(-19.1399177555961,21.7400087597643,
8.41309994443356));
#132920=CARTESIAN_POINT('Ctrl Pts',(-19.0565960387004,21.7505928405583,
8.41727862251751));
#132921=CARTESIAN_POINT('Ctrl Pts',(-18.9717808399116,21.7613666333938,
8.42153220040294));
#132922=CARTESIAN_POINT('Ctrl Pts',(-18.8863288596153,21.7678991601646,
8.42578577828838));
#132923=CARTESIAN_POINT('Ctrl Pts',(-18.8006993328509,21.7701309460434,
8.43003935617382));
#132924=CARTESIAN_POINT('Ctrl Pts',(-18.7167299015551,21.7723194643981,
8.43421047015177));
#132925=CARTESIAN_POINT('Ctrl Pts',(-18.6325902275832,21.7703724977257,
8.43838158412972));
#132926=CARTESIAN_POINT('Ctrl Pts',(-18.5487184100094,21.7642862613523,
8.44255269810767));
#132927=CARTESIAN_POINT('Ctrl Pts',(-18.4648747364341,21.7582020672743,
8.44672241242804));
#132928=CARTESIAN_POINT('Ctrl Pts',(-18.3812991991948,21.7479813952831,
8.45089212674842));
#132929=CARTESIAN_POINT('Ctrl Pts',(-18.2984275456889,21.7336725187874,
8.45506184106879));
#132930=CARTESIAN_POINT('Ctrl Pts',(-18.2155588411121,21.719364151463,8.45923140701283));
#132931=CARTESIAN_POINT('Ctrl Pts',(-18.1333944236485,21.7009679479898,
8.46340097295687));
#132932=CARTESIAN_POINT('Ctrl Pts',(-18.0523612259042,21.6785835510979,
8.46757053890091));
#132933=CARTESIAN_POINT('Ctrl Pts',(-17.9684790008924,21.6554121464255,
8.47188670163983));
#132934=CARTESIAN_POINT('Ctrl Pts',(-17.8858095314087,21.6279670209743,
8.47620286437875));
#132935=CARTESIAN_POINT('Ctrl Pts',(-17.8048088555661,21.5964148102805,
8.48051902711767));
#132936=CARTESIAN_POINT('Ctrl Pts',(-17.7264467682192,21.5658904095313,
8.48469459130935));
#132937=CARTESIAN_POINT('Ctrl Pts',(-17.6496468328974,21.5315226265231,
8.48887015550103));
#132938=CARTESIAN_POINT('Ctrl Pts',(-17.5747994654322,21.4935104864288,
8.49304571969271));
#132939=CARTESIAN_POINT('Ctrl Pts',(-17.496171735369,21.4535784435037,8.49743218170525));
#132940=CARTESIAN_POINT('Ctrl Pts',(-17.4196995115722,21.4096245062639,
8.5018186437178));
#132941=CARTESIAN_POINT('Ctrl Pts',(-17.3458018650431,21.3619314117614,
8.50620510573034));
#132942=CARTESIAN_POINT('Ctrl Pts',(-17.2719042185139,21.314238317259,8.51059156774288));
#132943=CARTESIAN_POINT('Ctrl Pts',(-17.200581575379,21.2628064665597,8.51497802975541));
#132944=CARTESIAN_POINT('Ctrl Pts',(-17.1322119090443,21.2079664272772,
8.51936449176795));
#132945=CARTESIAN_POINT('Ctrl Pts',(-17.0669880324057,21.1556496594946,
8.523549126161));
#132946=CARTESIAN_POINT('Ctrl Pts',(-17.004208586686,21.1000367097147,8.52773376055405));
#132947=CARTESIAN_POINT('Ctrl Pts',(-16.9442256444347,21.0413845924179,
8.5319183949471));
#132948=CARTESIAN_POINT('Ctrl Pts',(-16.8843280804773,20.9828159591503,
8.53609707303104));
#132949=CARTESIAN_POINT('Ctrl Pts',(-16.8272194396166,20.9212170697946,
8.54027575111499));
#132950=CARTESIAN_POINT('Ctrl Pts',(-16.7732194376017,20.8568856540237,
8.54445442919893));
#132951=CARTESIAN_POINT('Ctrl Pts',(-16.7182515243598,20.7914011438592,
8.54870800708437));
#132952=CARTESIAN_POINT('Ctrl Pts',(-16.6665051669309,20.7230854843409,
8.5529615849698));
#132953=CARTESIAN_POINT('Ctrl Pts',(-16.6182789494494,20.6522926268656,
8.55721516285524));
#132954=CARTESIAN_POINT('Ctrl Pts',(-16.5709876912995,20.5828722270732,
8.56138627683319));
#132955=CARTESIAN_POINT('Ctrl Pts',(-16.527081572471,20.5110702205223,8.56555739081114));
#132956=CARTESIAN_POINT('Ctrl Pts',(-16.4868009099953,20.4372529306314,
8.56972850478909));
#132957=CARTESIAN_POINT('Ctrl Pts',(-16.446533764085,20.363460410845,8.57389821910947));
#132958=CARTESIAN_POINT('Ctrl Pts',(-16.4098898786011,20.2876543542439,
8.57806793342984));
#132959=CARTESIAN_POINT('Ctrl Pts',(-16.3770645250476,20.2102272849111,
8.58223764775021));
#132960=CARTESIAN_POINT('Ctrl Pts',(-16.3442403395611,20.1328029707657,
8.58640721369426));
#132961=CARTESIAN_POINT('Ctrl Pts',(-16.3152345946181,20.0537581824513,
8.5905767796383));
#132962=CARTESIAN_POINT('Ctrl Pts',(-16.2901945969737,19.973505837446,8.59474634558234));
#132963=CARTESIAN_POINT('Ctrl Pts',(-16.2642742239022,19.8904319189922,
8.59906250832126));
#132964=CARTESIAN_POINT('Ctrl Pts',(-16.2426038152404,19.8060644520148,
8.60337867106019));
#132965=CARTESIAN_POINT('Ctrl Pts',(-16.225290101654,19.7208770890524,8.60769483379911));
#132966=CARTESIAN_POINT('Ctrl Pts',(-16.2085403804666,19.6384646954784,
8.61187039799079));
#132967=CARTESIAN_POINT('Ctrl Pts',(-16.1958678987932,19.5552854746203,
8.61604596218246));
#132968=CARTESIAN_POINT('Ctrl Pts',(-16.1873166326445,19.471775432959,8.62022152637414));
#132969=CARTESIAN_POINT('Ctrl Pts',(-16.1783334623714,19.3840474976197,
8.62460798838669));
#132970=CARTESIAN_POINT('Ctrl Pts',(-16.173898803398,19.2959550268228,8.62899445039923));
#132971=CARTESIAN_POINT('Ctrl Pts',(-16.1740017537922,19.2080034331647,
8.63338091241177));
#132972=CARTESIAN_POINT('Ctrl Pts',(-16.1741047041864,19.1200518395067,
8.63776737442431));
#132973=CARTESIAN_POINT('Ctrl Pts',(-16.1787451573697,19.0322416983818,
8.64215383643685));
#132974=CARTESIAN_POINT('Ctrl Pts',(-16.1878497481281,18.9450697555886,
8.64654029844939));
#132975=CARTESIAN_POINT('Ctrl Pts',(-16.1967810779015,18.8595567008307,
8.65084328578973));
#132976=CARTESIAN_POINT('Ctrl Pts',(-16.2100422563569,18.7743304265415,
8.65514627313006));
#132977=CARTESIAN_POINT('Ctrl Pts',(-16.2276047148296,18.6898640537483,
8.6594492604704));
#132978=CARTESIAN_POINT('Ctrl Pts',(-16.2446561859346,18.6078552668085,
8.66362705052256));
#132979=CARTESIAN_POINT('Ctrl Pts',(-16.2657620106882,18.526563267255,8.66780484057472));
#132980=CARTESIAN_POINT('Ctrl Pts',(-16.2908434939132,18.4464175735962,
8.67198263062689));
#132981=CARTESIAN_POINT('Ctrl Pts',(-16.3159003387464,18.3663506097709,
8.67615631669416));
#132982=CARTESIAN_POINT('Ctrl Pts',(-16.3449249508829,18.2874281524481,
8.68033000276144));
#132983=CARTESIAN_POINT('Ctrl Pts',(-16.3777879155978,18.2100681275347,
8.68450368882872));
#132984=CARTESIAN_POINT('Ctrl Pts',(-16.4106284573715,18.1327608866383,
8.68867452712137));
#132985=CARTESIAN_POINT('Ctrl Pts',(-16.4473019700395,18.0570143826501,
8.69284536541402));
#132986=CARTESIAN_POINT('Ctrl Pts',(-16.4876301165927,17.9832287074049,
8.69701620370667));
#132987=CARTESIAN_POINT('Ctrl Pts',(-16.5279428446235,17.9094712423847,
8.70118544737697));
#132988=CARTESIAN_POINT('Ctrl Pts',(-16.5719072084086,17.8376735188971,
8.70535469104727));
#132989=CARTESIAN_POINT('Ctrl Pts',(-16.6192985302658,17.7682118333227,
8.70952393471757));
#132990=CARTESIAN_POINT('Ctrl Pts',(-16.666700849621,17.6987340286633,8.71369414589093));
#132991=CARTESIAN_POINT('Ctrl Pts',(-16.7175314608585,17.6315937280806,
8.71786435706428));
#132992=CARTESIAN_POINT('Ctrl Pts',(-16.7715224094598,17.5671381728906,
8.72203456823764));
#132993=CARTESIAN_POINT('Ctrl Pts',(-16.8255216994708,17.5026726595463,
8.72620542369381));
#132994=CARTESIAN_POINT('Ctrl Pts',(-16.8826819940177,17.4408930619735,
8.73037627914997));
#132995=CARTESIAN_POINT('Ctrl Pts',(-16.9426963407412,17.3821120317728,
8.73454713460613));
#132996=CARTESIAN_POINT('Ctrl Pts',(-17.0027604759684,17.3232822362403,
8.73872145024579));
#132997=CARTESIAN_POINT('Ctrl Pts',(-17.0656830493498,17.2674562830652,
8.74289576588546));
#132998=CARTESIAN_POINT('Ctrl Pts',(-17.1311223695951,17.2149079926147,
8.74707008152512));
#132999=CARTESIAN_POINT('Ctrl Pts',(-17.145450381212,17.2034024862433,8.74798405255589));
#133000=CARTESIAN_POINT('Ctrl Pts',(-17.1598989273243,17.1920539496951,
8.74889802358666));
#133001=CARTESIAN_POINT('Ctrl Pts',(-17.174464231106,17.180864983421,8.74981199461743));
#133002=CARTESIAN_POINT('Ctrl Pts',(-17.1770150831773,17.1841768308936,
7.94987222090926));
#133003=CARTESIAN_POINT('Ctrl Pts',(-17.5010449670934,16.9346419658738,
7.97013523562024));
#133004=CARTESIAN_POINT('Ctrl Pts',(-18.6774627144846,16.3911012243001,
8.03279018589171));
#133005=CARTESIAN_POINT('Ctrl Pts',(-20.7208250384235,17.0720883649514,
8.12726281551246));
#133006=CARTESIAN_POINT('Ctrl Pts',(-21.28776986438,18.5735386239974,8.20147243042222));
#133007=CARTESIAN_POINT('Ctrl Pts',(-21.2935817164968,19.2133537193276,
8.23329010977151));
#133008=CARTESIAN_POINT('',(-21.2939989424941,19.2086731074563,8.16670989022852));
#133009=CARTESIAN_POINT('Ctrl Pts',(-17.171894433272,17.1775280041615,7.88329696157133));
#133010=CARTESIAN_POINT('Ctrl Pts',(-17.1803677644956,17.1710026187585,
7.88383131246386));
#133011=CARTESIAN_POINT('Ctrl Pts',(-17.8646300971893,16.6514603543991,
7.92675759891687));
#133012=CARTESIAN_POINT('Ctrl Pts',(-19.7898863352068,16.3740305446598,
8.01207582093035));
#133013=CARTESIAN_POINT('Ctrl Pts',(-21.194097770004,17.9910561083639,8.10601244625689));
#133014=CARTESIAN_POINT('Ctrl Pts',(-21.29615524784,19.0247813417565,8.15755713602294));
#133015=CARTESIAN_POINT('Ctrl Pts',(-21.2944497293802,19.2086726977168,
8.16670989022852));
#133016=CARTESIAN_POINT('Ctrl Pts',(-21.2939989424941,19.2086731074563,
8.16670989022852));
#133017=CARTESIAN_POINT('Ctrl Pts',(-21.294074804776,19.2921352174732,8.17086478789788));
#133018=CARTESIAN_POINT('Ctrl Pts',(-21.2900646933588,19.3757219830021,
8.17501968556724));
#133019=CARTESIAN_POINT('Ctrl Pts',(-21.2819596922617,19.458994771335,8.17917458323661));
#133020=CARTESIAN_POINT('Ctrl Pts',(-21.2739328413916,19.5414646248839,
8.18328941845664));
#133021=CARTESIAN_POINT('Ctrl Pts',(-21.2618897634889,19.6236260477268,
8.18740425367667));
#133022=CARTESIAN_POINT('Ctrl Pts',(-21.2458740550218,19.7050533692914,
8.1915190888967));
#133023=CARTESIAN_POINT('Ctrl Pts',(-21.229865310909,19.7864452825742,8.19563213480029));
#133024=CARTESIAN_POINT('Ctrl Pts',(-21.2098874553345,19.867103263636,8.19974518070388));
#133025=CARTESIAN_POINT('Ctrl Pts',(-21.1860355605652,19.9466096857189,
8.20385822660747));
#133026=CARTESIAN_POINT('Ctrl Pts',(-21.1621864189586,20.0261069305809,
8.2079707977528));
#133027=CARTESIAN_POINT('Ctrl Pts',(-21.1344642632168,20.1044524267967,
8.21208336889812));
#133028=CARTESIAN_POINT('Ctrl Pts',(-21.1030141994638,20.1812431255818,
8.21619594004345));
#133029=CARTESIAN_POINT('Ctrl Pts',(-21.0710029255604,20.2594041147406,
8.2203818978976));
#133030=CARTESIAN_POINT('Ctrl Pts',(-21.0351295718013,20.3359537977659,
8.22456785575175));
#133031=CARTESIAN_POINT('Ctrl Pts',(-20.9955977974884,20.4104896424712,
8.22875381360589));
#133032=CARTESIAN_POINT('Ctrl Pts',(-20.9567081892514,20.4838147044139,
8.23287177349699));
#133033=CARTESIAN_POINT('Ctrl Pts',(-20.9142784405329,20.5551904907364,
8.23698973338808));
#133034=CARTESIAN_POINT('Ctrl Pts',(-20.8685472200438,20.624261534679,8.24110769327918));
#133035=CARTESIAN_POINT('Ctrl Pts',(-20.8216832918827,20.6950433858241,
8.24532765011485));
#133036=CARTESIAN_POINT('Ctrl Pts',(-20.7713524862058,20.7634043768936,
8.24954760695052));
#133037=CARTESIAN_POINT('Ctrl Pts',(-20.7178552814756,20.8289982145112,
8.2537675637862));
#133038=CARTESIAN_POINT('Ctrl Pts',(-20.6643580767454,20.8945920521287,
8.25798752062187));
#133039=CARTESIAN_POINT('Ctrl Pts',(-20.6076948817588,20.9574183953714,
8.26220747745755));
#133040=CARTESIAN_POINT('Ctrl Pts',(-20.5482046419776,21.0171731691692,
8.26642743429322));
#133041=CARTESIAN_POINT('Ctrl Pts',(-20.4892123552949,21.0764277756309,
8.27061206868627));
#133042=CARTESIAN_POINT('Ctrl Pts',(-20.4272042190729,21.1328994502154,
8.27479670307932));
#133043=CARTESIAN_POINT('Ctrl Pts',(-20.3624734272384,21.1862656268913,
8.27898133747237));
#133044=CARTESIAN_POINT('Ctrl Pts',(-20.297834771674,21.2395558434202,8.28316001555632));
#133045=CARTESIAN_POINT('Ctrl Pts',(-20.2304815101079,21.2897490519969,
8.28733869364026));
#133046=CARTESIAN_POINT('Ctrl Pts',(-20.1607438576393,21.3365592122283,
8.29151737172421));
#133047=CARTESIAN_POINT('Ctrl Pts',(-20.0897562078699,21.3842084109399,
8.29577094960965));
#133048=CARTESIAN_POINT('Ctrl Pts',(-20.0162981861696,21.4283517444168,
8.30002452749508));
#133049=CARTESIAN_POINT('Ctrl Pts',(-19.9407536469186,21.4687301954947,
8.30427810538052));
#133050=CARTESIAN_POINT('Ctrl Pts',(-19.866673685974,21.5083258315064,8.30844921935847));
#133051=CARTESIAN_POINT('Ctrl Pts',(-19.7905878123474,21.5443010347692,
8.31262033333642));
#133052=CARTESIAN_POINT('Ctrl Pts',(-19.7128859499198,21.5764560442015,
8.31679144731437));
#133053=CARTESIAN_POINT('Ctrl Pts',(-19.6352101611025,21.6086002637099,
8.32096116163474));
#133054=CARTESIAN_POINT('Ctrl Pts',(-19.555919885142,21.6369266595076,8.32513087595511));
#133055=CARTESIAN_POINT('Ctrl Pts',(-19.4754262787738,21.6612830598002,
8.32930059027549));
#133056=CARTESIAN_POINT('Ctrl Pts',(-19.3949355367136,21.6856385933875,
8.33347015621952));
#133057=CARTESIAN_POINT('Ctrl Pts',(-19.3132419899458,21.7060242799308,
8.33763972216356));
#133058=CARTESIAN_POINT('Ctrl Pts',(-19.2307719418924,21.7223378183248,
8.3418092881076));
#133059=CARTESIAN_POINT('Ctrl Pts',(-19.145402348687,21.7392249206038,8.34612545084652));
#133060=CARTESIAN_POINT('Ctrl Pts',(-19.0592011520728,21.7517480910506,
8.35044161358545));
#133061=CARTESIAN_POINT('Ctrl Pts',(-18.9726507026519,21.7598518674344,
8.35475777632437));
#133062=CARTESIAN_POINT('Ctrl Pts',(-18.8889196250174,21.7676916641548,
8.35893334051605));
#133063=CARTESIAN_POINT('Ctrl Pts',(-18.8048621716343,21.7713955951849,
8.36310890470773));
#133064=CARTESIAN_POINT('Ctrl Pts',(-18.7209165514645,21.770966566847,8.36728446889941));
#133065=CARTESIAN_POINT('Ctrl Pts',(-18.6327310375816,21.7705158693076,
8.37167093091195));
#133066=CARTESIAN_POINT('Ctrl Pts',(-18.5446695341431,21.7655037616187,
8.37605739292449));
#133067=CARTESIAN_POINT('Ctrl Pts',(-18.4572333890564,21.7559951361578,
8.38044385493703));
#133068=CARTESIAN_POINT('Ctrl Pts',(-18.3697972439697,21.7464865106968,
8.38483031694958));
#133069=CARTESIAN_POINT('Ctrl Pts',(-18.2829870179306,21.7324815349687,
8.38921677896212));
#133070=CARTESIAN_POINT('Ctrl Pts',(-18.1972887614195,21.7141062794818,
8.39360324097466));
#133071=CARTESIAN_POINT('Ctrl Pts',(-18.1155336087259,21.6965764967386,
8.39778787536772));
#133072=CARTESIAN_POINT('Ctrl Pts',(-18.034486039177,21.6750045135588,8.40197250976076));
#133073=CARTESIAN_POINT('Ctrl Pts',(-17.9545759800696,21.649462260761,8.40615714415381));
#133074=CARTESIAN_POINT('Ctrl Pts',(-17.8747796630406,21.6239563641985,
8.41033582223775));
#133075=CARTESIAN_POINT('Ctrl Pts',(-17.7961180748451,21.5944915619193,
8.41451450032169));
#133076=CARTESIAN_POINT('Ctrl Pts',(-17.7190104693571,21.5611906843244,
8.41869317840563));
#133077=CARTESIAN_POINT('Ctrl Pts',(-17.6405207654569,21.5272929124315,
8.42294675629106));
#133078=CARTESIAN_POINT('Ctrl Pts',(-17.5636417739319,21.4894202903321,
8.4272003341765));
#133079=CARTESIAN_POINT('Ctrl Pts',(-17.4887990603227,21.4477553777351,
8.43145391206194));
#133080=CARTESIAN_POINT('Ctrl Pts',(-17.4154073187604,21.4068982207712,
8.43562502603989));
#133081=CARTESIAN_POINT('Ctrl Pts',(-17.3439740257043,21.3623947371042,
8.43979614001785));
#133082=CARTESIAN_POINT('Ctrl Pts',(-17.2748782070125,21.3144646641265,
8.4439672539958));
#133083=CARTESIAN_POINT('Ctrl Pts',(-17.2058055740901,21.2665506745478,
8.44813696831618));
#133084=CARTESIAN_POINT('Ctrl Pts',(-17.1390692354552,21.2152126412159,
8.45230668263655));
#133085=CARTESIAN_POINT('Ctrl Pts',(-17.0750196948479,21.1607139141724,
8.45647639695692));
#133086=CARTESIAN_POINT('Ctrl Pts',(-17.0109724333982,21.1062171264274,
8.46064596290096));
#133087=CARTESIAN_POINT('Ctrl Pts',(-16.9496121296953,21.0485601673606,
8.464815528845));
#133088=CARTESIAN_POINT('Ctrl Pts',(-16.8912555527362,20.9880461170376,
8.46898509478904));
#133089=CARTESIAN_POINT('Ctrl Pts',(-16.8308472305218,20.9254044673573,
8.47330125752796));
#133090=CARTESIAN_POINT('Ctrl Pts',(-16.7736581532185,20.859701457282,8.47761742026688));
#133091=CARTESIAN_POINT('Ctrl Pts',(-16.7199960430177,20.7913126466809,
8.4819335830058));
#133092=CARTESIAN_POINT('Ctrl Pts',(-16.6680819704125,20.7251515943919,
8.48610914719748));
#133093=CARTESIAN_POINT('Ctrl Pts',(-16.6194688453354,20.6564774460931,
8.49028471138916));
#133094=CARTESIAN_POINT('Ctrl Pts',(-16.5743914182291,20.5856602393105,
8.49446027558084));
#133095=CARTESIAN_POINT('Ctrl Pts',(-16.527037237441,20.5112662237653,8.49884673759338));
#133096=CARTESIAN_POINT('Ctrl Pts',(-16.4835856052314,20.4345074765787,
8.50323319960592));
#133097=CARTESIAN_POINT('Ctrl Pts',(-16.4442533274937,20.3558406770141,
8.50761966161846));
#133098=CARTESIAN_POINT('Ctrl Pts',(-16.4049210497559,20.2771738774495,
8.51200612363101));
#133099=CARTESIAN_POINT('Ctrl Pts',(-16.369708289139,20.1965995876304,8.51639258564355));
#133100=CARTESIAN_POINT('Ctrl Pts',(-16.3387721302028,20.1145947386671,
8.52077904765609));
#133101=CARTESIAN_POINT('Ctrl Pts',(-16.3092593897977,20.0363630543649,
8.52496368204914));
#133102=CARTESIAN_POINT('Ctrl Pts',(-16.2835285016034,19.9565383690801,
8.52914831644219));
#133103=CARTESIAN_POINT('Ctrl Pts',(-16.2617516946766,19.8755211184195,
8.53333295083523));
#133104=CARTESIAN_POINT('Ctrl Pts',(-16.240005884339,19.7946191857874,8.53751162891917));
#133105=CARTESIAN_POINT('Ctrl Pts',(-16.2222030943946,19.7125284999517,
8.54169030700311));
#133106=CARTESIAN_POINT('Ctrl Pts',(-16.2084669780845,19.6296680728384,
8.54586898508705));
#133107=CARTESIAN_POINT('Ctrl Pts',(-16.1944846517615,19.5453224321197,
8.55012256297248));
#133108=CARTESIAN_POINT('Ctrl Pts',(-16.1847163934877,19.4601796345801,
8.55437614085792));
#133109=CARTESIAN_POINT('Ctrl Pts',(-16.179239049994,19.3746963295997,8.55862971874336));
#133110=CARTESIAN_POINT('Ctrl Pts',(-16.1738678954921,19.2908702852934,
8.56280083272131));
#133111=CARTESIAN_POINT('Ctrl Pts',(-16.1726227957354,19.2067172987634,
8.56697194669926));
#133112=CARTESIAN_POINT('Ctrl Pts',(-16.1755241458591,19.1226750104571,
8.57114306067721));
#133113=CARTESIAN_POINT('Ctrl Pts',(-16.1784245224067,19.0386609233523,
8.57531277499758));
#133114=CARTESIAN_POINT('Ctrl Pts',(-16.1854685696705,18.9547579200753,
8.57948248931794));
#133115=CARTESIAN_POINT('Ctrl Pts',(-16.1966245729685,18.8714032651857,
8.58365220363831));
#133116=CARTESIAN_POINT('Ctrl Pts',(-16.207780179288,18.7880515764123,8.58782176958235));
#133117=CARTESIAN_POINT('Ctrl Pts',(-16.2230473888474,18.7052486530845,
8.5919913355264));
#133118=CARTESIAN_POINT('Ctrl Pts',(-16.242342820325,18.6234248992902,8.59616090147044));
#133119=CARTESIAN_POINT('Ctrl Pts',(-16.2623166553699,18.538724323253,8.60047706420936));
#133120=CARTESIAN_POINT('Ctrl Pts',(-16.2866071262488,18.455073566411,8.60479322694829));
#133121=CARTESIAN_POINT('Ctrl Pts',(-16.3150650107312,18.3729346578631,
8.60910938968721));
#133122=CARTESIAN_POINT('Ctrl Pts',(-16.3425958826198,18.2934714156217,
8.6132849538789));
#133123=CARTESIAN_POINT('Ctrl Pts',(-16.3740266108361,18.2154234566597,
8.61746051807058));
#133124=CARTESIAN_POINT('Ctrl Pts',(-16.4091731183427,18.1391884632439,
8.62163608226227));
#133125=CARTESIAN_POINT('Ctrl Pts',(-16.4460947923905,18.059103021542,8.62602254427481));
#133126=CARTESIAN_POINT('Ctrl Pts',(-16.4871172070497,17.9810190212164,
8.63040900628735));
#133127=CARTESIAN_POINT('Ctrl Pts',(-16.5319737202488,17.9053659535363,
8.6347954682999));
#133128=CARTESIAN_POINT('Ctrl Pts',(-16.576830233448,17.8297128858562,8.63918193031244));
#133129=CARTESIAN_POINT('Ctrl Pts',(-16.6255204605689,17.7564911918507,
8.64356839232499));
#133130=CARTESIAN_POINT('Ctrl Pts',(-16.677728404917,17.6860911085397,8.64795485433754));
#133131=CARTESIAN_POINT('Ctrl Pts',(-16.7275305668981,17.6189351153988,
8.6521391847953));
#133132=CARTESIAN_POINT('Ctrl Pts',(-16.7807187430267,17.5540964632713,
8.65632351525307));
#133133=CARTESIAN_POINT('Ctrl Pts',(-16.8370495093169,17.491936639941,8.66050784571084));
#133134=CARTESIAN_POINT('Ctrl Pts',(-16.8932939076247,17.4298721218744,
8.66468576063046));
#133135=CARTESIAN_POINT('Ctrl Pts',(-16.952671014844,17.3704786082901,8.66886367555008));
#133136=CARTESIAN_POINT('Ctrl Pts',(-17.0148956024391,17.3140866993226,
8.6730415904697));
#133137=CARTESIAN_POINT('Ctrl Pts',(-17.0662095397694,17.2675827208387,
8.67648693695801));
#133138=CARTESIAN_POINT('Ctrl Pts',(-17.1194590718192,17.2231195687963,
8.67993228344631));
#133139=CARTESIAN_POINT('Ctrl Pts',(-17.174464231106,17.180864983421,8.68337762993461));
#133140=CARTESIAN_POINT('Origin',(-18.734,19.211,-1.76670989022852));
#133141=CARTESIAN_POINT('',(-17.1725834074896,17.1783793283469,9.54996332099649));
#133142=CARTESIAN_POINT('',(-17.174464231106,17.180864983421,9.48328065598191));
#133143=CARTESIAN_POINT('',(-17.174464231106,17.180864983421,-1.76670989022852));
#133144=CARTESIAN_POINT('',(-21.2943302600992,19.210357489227,9.03329016591285));
#133145=CARTESIAN_POINT('Ctrl Pts',(-21.2980344970333,19.2103691601534,
9.03329079544681));
#133146=CARTESIAN_POINT('Ctrl Pts',(-21.2952860334465,20.0241271385548,
9.07394170535625));
#133147=CARTESIAN_POINT('Ctrl Pts',(-20.4360629396139,21.691476034616,9.15698455082618));
#133148=CARTESIAN_POINT('Ctrl Pts',(-17.5947352470201,22.0155262669008,
9.28241933185656));
#133149=CARTESIAN_POINT('Ctrl Pts',(-15.7591748325173,19.7710955115256,
9.40959513853801));
#133150=CARTESIAN_POINT('Ctrl Pts',(-16.3858468785065,17.8368644049063,
9.49877646825131));
#133151=CARTESIAN_POINT('Ctrl Pts',(-17.1023021432777,17.2315279292858,
9.54556586240414));
#133152=CARTESIAN_POINT('Ctrl Pts',(-17.1725834074896,17.1783793283469,
9.54996332099649));
#133153=CARTESIAN_POINT('Ctrl Pts',(-17.174464231106,17.180864983421,8.74981199461743));
#133154=CARTESIAN_POINT('Ctrl Pts',(-17.2411338659978,17.1296498280428,
8.75399550605232));
#133155=CARTESIAN_POINT('Ctrl Pts',(-17.3102517202361,17.0817815881081,
8.7581790174872));
#133156=CARTESIAN_POINT('Ctrl Pts',(-17.3814398259537,17.0374818897502,
8.76236252892209));
#133157=CARTESIAN_POINT('Ctrl Pts',(-17.4458386446654,16.9974071017674,
8.766147054325));
#133158=CARTESIAN_POINT('Ctrl Pts',(-17.5119310943407,16.9602521707291,
8.76993157972792));
#133159=CARTESIAN_POINT('Ctrl Pts',(-17.5794224113971,16.926147577655,8.77371610513083));
#133160=CARTESIAN_POINT('Ctrl Pts',(-17.6540490703618,16.8884373662162,
8.77790073952388));
#133161=CARTESIAN_POINT('Ctrl Pts',(-17.730664056125,16.8543169479217,8.78208537391692));
#133162=CARTESIAN_POINT('Ctrl Pts',(-17.8088876493305,16.8240003898956,
8.78627000830997));
#133163=CARTESIAN_POINT('Ctrl Pts',(-17.8869999009332,16.7937269837373,
8.79044868639392));
#133164=CARTESIAN_POINT('Ctrl Pts',(-17.9667157867297,16.7672468481168,
8.79462736447786));
#133165=CARTESIAN_POINT('Ctrl Pts',(-18.0476319224909,16.7447277396491,
8.79880604256181));
#133166=CARTESIAN_POINT('Ctrl Pts',(-18.1299984218322,16.7218049923463,
8.80305962044724));
#133167=CARTESIAN_POINT('Ctrl Pts',(-18.213608193011,16.7029868892008,8.80731319833267));
#133168=CARTESIAN_POINT('Ctrl Pts',(-18.2980154243377,16.6883986740302,
8.81156677621811));
#133169=CARTESIAN_POINT('Ctrl Pts',(-18.380786256778,16.6740932798773,8.81573789019606));
#133170=CARTESIAN_POINT('Ctrl Pts',(-18.4643234304655,16.6638553099794,
8.81990900417401));
#133171=CARTESIAN_POINT('Ctrl Pts',(-18.5481939962223,16.6577518473599,
8.82408011815197));
#133172=CARTESIAN_POINT('Ctrl Pts',(-18.6320364184008,16.6516504328163,
8.82824983247234));
#133173=CARTESIAN_POINT('Ctrl Pts',(-18.7162115520294,16.6496808035662,
8.83241954679271));
#133174=CARTESIAN_POINT('Ctrl Pts',(-18.8002812486104,16.6518581914863,
8.83658926111308));
#133175=CARTESIAN_POINT('Ctrl Pts',(-18.8843479536308,16.6540355019256,
8.84075882705713));
#133176=CARTESIAN_POINT('Ctrl Pts',(-18.9683087692067,16.660359523368,8.84492839300117));
#133177=CARTESIAN_POINT('Ctrl Pts',(-19.0517268423097,16.6707933836643,
8.84909795894522));
#133178=CARTESIAN_POINT('Ctrl Pts',(-19.1380777919556,16.681594085617,8.85341412168414));
#133179=CARTESIAN_POINT('Ctrl Pts',(-19.2238466000237,16.6967989420232,
8.85773028442306));
#133180=CARTESIAN_POINT('Ctrl Pts',(-19.3085579282895,16.7163089996876,
8.86204644716198));
#133181=CARTESIAN_POINT('Ctrl Pts',(-19.3905097939472,16.7351835192757,
8.86622201135366));
#133182=CARTESIAN_POINT('Ctrl Pts',(-19.4714715762059,16.758086889941,8.87039757554534));
#133183=CARTESIAN_POINT('Ctrl Pts',(-19.551028186959,16.7848786218092,8.87457313973702));
#133184=CARTESIAN_POINT('Ctrl Pts',(-19.6346030129933,16.8130235403628,
8.87895960174956));
#133185=CARTESIAN_POINT('Ctrl Pts',(-19.716626443602,16.8454597306831,8.8833460637621));
#133186=CARTESIAN_POINT('Ctrl Pts',(-19.7966429339306,16.8819680133224,
8.88773252577464));
#133187=CARTESIAN_POINT('Ctrl Pts',(-19.8766594242591,16.9184762959617,
8.89211898778718));
#133188=CARTESIAN_POINT('Ctrl Pts',(-19.9546684946739,16.959056335675,8.89650544979972));
#133189=CARTESIAN_POINT('Ctrl Pts',(-20.0302483510423,17.003435683288,8.90089191181226));
#133190=CARTESIAN_POINT('Ctrl Pts',(-20.102350666183,17.0457730713314,8.90507654620531));
#133191=CARTESIAN_POINT('Ctrl Pts',(-20.1725107769709,17.0917254144961,
8.90926118059836));
#133192=CARTESIAN_POINT('Ctrl Pts',(-20.240343151946,17.1410892993693,8.91344581499141));
#133193=CARTESIAN_POINT('Ctrl Pts',(-20.3080789759311,17.1903829208624,
8.91762449307535));
#133194=CARTESIAN_POINT('Ctrl Pts',(-20.373493276466,17.243078170329,8.9218031711593));
#133195=CARTESIAN_POINT('Ctrl Pts',(-20.4362266525528,17.2989266689431,
8.92598184924324));
#133196=CARTESIAN_POINT('Ctrl Pts',(-20.5000844793203,17.3557762117573,
8.93023542712868));
#133197=CARTESIAN_POINT('Ctrl Pts',(-20.5611639093906,17.4158929154665,
8.93448900501411));
#133198=CARTESIAN_POINT('Ctrl Pts',(-20.6191183231213,17.4789697150938,
8.93874258289955));
#133199=CARTESIAN_POINT('Ctrl Pts',(-20.6759491774531,17.5408236478761,
8.9429136968775));
#133200=CARTESIAN_POINT('Ctrl Pts',(-20.7297747776526,17.6055235719756,
8.94708481085545));
#133201=CARTESIAN_POINT('Ctrl Pts',(-20.7803043703348,17.6727417564177,
8.9512559248334));
#133202=CARTESIAN_POINT('Ctrl Pts',(-20.8308170073241,17.7399373851488,
8.95542563915377));
#133203=CARTESIAN_POINT('Ctrl Pts',(-20.8780355571482,17.8096492285708,
8.95959535347414));
#133204=CARTESIAN_POINT('Ctrl Pts',(-20.9217100507379,17.8815171178612,
8.96376506779451));
#133205=CARTESIAN_POINT('Ctrl Pts',(-20.9653829902017,17.9533824497836,
8.96793463373855));
#133206=CARTESIAN_POINT('Ctrl Pts',(-21.0055118859952,18.0274032814579,
8.9721041996826));
#133207=CARTESIAN_POINT('Ctrl Pts',(-21.0418912815019,18.1031923304257,
8.97627376562664));
#133208=CARTESIAN_POINT('Ctrl Pts',(-21.0795497316758,18.1816460288594,
8.98058992836556));
#133209=CARTESIAN_POINT('Ctrl Pts',(-21.1131898827321,18.2619941236263,
8.98490609110448));
#133210=CARTESIAN_POINT('Ctrl Pts',(-21.1426376470828,18.3437833690158,
8.9892222538434));
#133211=CARTESIAN_POINT('Ctrl Pts',(-21.171126153607,18.4229083383394,8.99339781803508));
#133212=CARTESIAN_POINT('Ctrl Pts',(-21.1956911205896,18.5033815448835,
8.99757338222676));
#133213=CARTESIAN_POINT('Ctrl Pts',(-21.2162259984621,18.5847779207351,
9.00174894641844));
#133214=CARTESIAN_POINT('Ctrl Pts',(-21.2377980441989,18.6702854340294,
9.00613540843098));
#133215=CARTESIAN_POINT('Ctrl Pts',(-21.254922068569,18.7568112533014,9.01052187044352));
#133216=CARTESIAN_POINT('Ctrl Pts',(-21.2675357890124,18.8438536997419,
9.01490833245606));
#133217=CARTESIAN_POINT('Ctrl Pts',(-21.2801495094559,18.9308961461825,
9.01929479446861));
#133218=CARTESIAN_POINT('Ctrl Pts',(-21.288252948244,19.0184546350337,9.02368125648114));
#133219=CARTESIAN_POINT('Ctrl Pts',(-21.2918468828523,19.10602703261,9.02806771849369));
#133220=CARTESIAN_POINT('Ctrl Pts',(-21.2932731600888,19.1407807303868,
9.02980851558629));
#133221=CARTESIAN_POINT('Ctrl Pts',(-21.2939911726516,19.1755636940745,
9.0315493126789));
#133222=CARTESIAN_POINT('Ctrl Pts',(-21.2939999191096,19.2103564484228,
9.0332901097715));
#133223=CARTESIAN_POINT('',(-21.293999998394,19.2110906788005,8.96670989026365));
#133224=CARTESIAN_POINT('Ctrl Pts',(-17.174464231106,17.180864983421,8.68337762993461));
#133225=CARTESIAN_POINT('Ctrl Pts',(-17.2410629602576,17.1297042973452,
8.68754916039799));
#133226=CARTESIAN_POINT('Ctrl Pts',(-17.3102360430907,17.0817825735557,
8.69172069086136));
#133227=CARTESIAN_POINT('Ctrl Pts',(-17.3816325649282,17.0373619619271,
8.69589222132474));
#133228=CARTESIAN_POINT('Ctrl Pts',(-17.4530009748456,16.9929588406279,
8.70006210927489));
#133229=CARTESIAN_POINT('Ctrl Pts',(-17.526590695086,16.952054336701,8.70423199722505));
#133230=CARTESIAN_POINT('Ctrl Pts',(-17.6020218660579,16.9148672720688,
8.70840188517521));
#133231=CARTESIAN_POINT('Ctrl Pts',(-17.6774459640613,16.8776836943628,
8.71257138212671));
#133232=CARTESIAN_POINT('Ctrl Pts',(-17.7547107568408,16.844217066174,8.71674087907822));
#133233=CARTESIAN_POINT('Ctrl Pts',(-17.8334130523661,16.8146396035338,
8.72091037602972));
#133234=CARTESIAN_POINT('Ctrl Pts',(-17.9121315766146,16.7850560419044,
8.72508073274792));
#133235=CARTESIAN_POINT('Ctrl Pts',(-17.9922877611872,16.7593633988364,
8.72925108946611));
#133236=CARTESIAN_POINT('Ctrl Pts',(-18.0734610672701,16.7376847515232,
8.7334214461843));
#133237=CARTESIAN_POINT('Ctrl Pts',(-18.1547254427102,16.7159817826617,
8.73759648167837));
#133238=CARTESIAN_POINT('Ctrl Pts',(-18.2370087716157,16.6983019143779,
8.74177151717243));
#133239=CARTESIAN_POINT('Ctrl Pts',(-18.3198786279348,16.684717456578,8.7459465526665));
#133240=CARTESIAN_POINT('Ctrl Pts',(-18.4028029852764,16.6711240646871,
8.75012433395637));
#133241=CARTESIAN_POINT('Ctrl Pts',(-18.4863141811532,16.6616314953346,
8.75430211524624));
#133242=CARTESIAN_POINT('Ctrl Pts',(-18.5699753170643,16.6562601104246,
8.75847989653611));
#133243=CARTESIAN_POINT('Ctrl Pts',(-18.6537710890963,16.6508800813285,
8.76266440114214));
#133244=CARTESIAN_POINT('Ctrl Pts',(-18.7377168237858,16.6496344772215,
8.76684890574817));
#133245=CARTESIAN_POINT('Ctrl Pts',(-18.8213768080935,16.6524915881695,
8.77103341035419));
#133246=CARTESIAN_POINT('Ctrl Pts',(-18.8486819858539,16.6534240999667,
8.77239916057579));
#133247=CARTESIAN_POINT('Ctrl Pts',(-18.8759567793247,16.6547932460373,
8.77376491079738));
#133248=CARTESIAN_POINT('Ctrl Pts',(-18.903186241511,16.6565967398073,8.77513066101897));
#133249=CARTESIAN_POINT('Ctrl Pts',(-18.9866168294529,16.6621226126484,
8.77931529541202));
#133250=CARTESIAN_POINT('Ctrl Pts',(-19.0699316687707,16.6717505167587,
8.78349992980507));
#133251=CARTESIAN_POINT('Ctrl Pts',(-19.1526949496535,16.6854714337124,
8.78768456419812));
#133252=CARTESIAN_POINT('Ctrl Pts',(-19.23534042725,16.6991728206392,8.79186324228206));
#133253=CARTESIAN_POINT('Ctrl Pts',(-19.3174354558612,16.7169555737484,
8.79604192036601));
#133254=CARTESIAN_POINT('Ctrl Pts',(-19.3985474281628,16.7387587666811,
8.80022059844996));
#133255=CARTESIAN_POINT('Ctrl Pts',(-19.4811132742737,16.7609527661774,
8.8044741763354));
#133256=CARTESIAN_POINT('Ctrl Pts',(-19.5626599937769,16.7873127240843,
8.80872775422083));
#133257=CARTESIAN_POINT('Ctrl Pts',(-19.6427400986364,16.8177195247673,
8.81298133210626));
#133258=CARTESIAN_POINT('Ctrl Pts',(-19.7212676943998,16.847536830285,8.81715244608422));
#133259=CARTESIAN_POINT('Ctrl Pts',(-19.7983845845479,16.8812452961239,
8.82132356006216));
#133260=CARTESIAN_POINT('Ctrl Pts',(-19.8736839568168,16.9186822910917,
8.82549467404011));
#133261=CARTESIAN_POINT('Ctrl Pts',(-19.9489580616541,16.9561067237144,
8.82966438836048));
#133262=CARTESIAN_POINT('Ctrl Pts',(-20.0224154482673,16.9972569960432,
8.83383410268086));
#133263=CARTESIAN_POINT('Ctrl Pts',(-20.0936712215606,17.0419231988563,
8.83800381700123));
#133264=CARTESIAN_POINT('Ctrl Pts',(-20.1649244592674,17.086587812254,8.84217338294525));
#133265=CARTESIAN_POINT('Ctrl Pts',(-20.2339758500889,17.1347678623259,
8.84634294888928));
#133266=CARTESIAN_POINT('Ctrl Pts',(-20.3004681352879,17.186209250039,8.85051251483331));
#133267=CARTESIAN_POINT('Ctrl Pts',(-20.3692982072077,17.2394592534845,
8.85482867757223));
#133268=CARTESIAN_POINT('Ctrl Pts',(-20.4353854517824,17.2962038761398,
8.85914484031115));
#133269=CARTESIAN_POINT('Ctrl Pts',(-20.4983710832762,17.3561159927104,
8.86346100305008));
#133270=CARTESIAN_POINT('Ctrl Pts',(-20.5593049644491,17.4140764783854,
8.86763656724176));
#133271=CARTESIAN_POINT('Ctrl Pts',(-20.6173359087925,17.4750008911685,
8.87181213143345));
#133272=CARTESIAN_POINT('Ctrl Pts',(-20.6721781340604,17.5385570202096,
8.87598769562513));
#133273=CARTESIAN_POINT('Ctrl Pts',(-20.7297903097516,17.6053232182383,
8.88037415763768));
#133274=CARTESIAN_POINT('Ctrl Pts',(-20.7838828183067,17.6749935141293,
8.88476061965022));
#133275=CARTESIAN_POINT('Ctrl Pts',(-20.8341751072843,17.7471473712346,
8.88914708166276));
#133276=CARTESIAN_POINT('Ctrl Pts',(-20.8844673962619,17.8193012283399,
8.89353354367531));
#133277=CARTESIAN_POINT('Ctrl Pts',(-20.930959223453,17.8939381139567,8.89792000568785));
#133278=CARTESIAN_POINT('Ctrl Pts',(-20.9734262024012,17.9706088181549,
8.9023064677004));
#133279=CARTESIAN_POINT('Ctrl Pts',(-21.0159038253685,18.047298739271,8.90669402914565));
#133280=CARTESIAN_POINT('Ctrl Pts',(-21.054500797719,18.1262856298352,8.91108159059091));
#133281=CARTESIAN_POINT('Ctrl Pts',(-21.0889748257326,18.2071605854691,
8.91546915203617));
#133282=CARTESIAN_POINT('Ctrl Pts',(-21.1233545067053,18.2878142059939,
8.91984470579149));
#133283=CARTESIAN_POINT('Ctrl Pts',(-21.1536335666927,18.3703452363822,
8.92422025954681));
#133284=CARTESIAN_POINT('Ctrl Pts',(-21.1796158858341,18.4543211123894,
8.92859581330213));
#133285=CARTESIAN_POINT('Ctrl Pts',(-21.2055560013422,18.5381605845955,
8.93296425975244));
#133286=CARTESIAN_POINT('Ctrl Pts',(-21.2272131436812,18.6234398583861,
8.93733270620275));
#133287=CARTESIAN_POINT('Ctrl Pts',(-21.2444392039475,18.7097066694204,
8.94170115265306));
#133288=CARTESIAN_POINT('Ctrl Pts',(-21.2616295048393,18.7957944002037,
8.94606053069714));
#133289=CARTESIAN_POINT('Ctrl Pts',(-21.274406969619,18.8828651985172,8.95041990874123));
#133290=CARTESIAN_POINT('Ctrl Pts',(-21.2826736357252,18.9704533339265,
8.95477928678531));
#133291=CARTESIAN_POINT('Ctrl Pts',(-21.2902149496553,19.0503561166423,
8.95875615459971));
#133292=CARTESIAN_POINT('Ctrl Pts',(-21.2940028463113,19.1306890276033,
8.96273302241411));
#133293=CARTESIAN_POINT('Ctrl Pts',(-21.293999998394,19.2110906780901,8.96670989022851));
#133294=CARTESIAN_POINT('Ctrl Pts',(-21.293999998394,19.2110906788005,8.96670989026365));
#133295=CARTESIAN_POINT('Ctrl Pts',(-21.2939968622716,19.2996281672638,
8.97108917708311));
#133296=CARTESIAN_POINT('Ctrl Pts',(-21.2893963356695,19.3880718027693,
8.97546846390256));
#133297=CARTESIAN_POINT('Ctrl Pts',(-21.2802532223815,19.4759424985004,
8.97984775072202));
#133298=CARTESIAN_POINT('Ctrl Pts',(-21.2710840473103,19.5640636632957,
8.98423952038189));
#133299=CARTESIAN_POINT('Ctrl Pts',(-21.2573464424813,19.6516082364874,
8.98863129004176));
#133300=CARTESIAN_POINT('Ctrl Pts',(-21.2391468026208,19.7381048257401,
8.99302305970162));
#133301=CARTESIAN_POINT('Ctrl Pts',(-21.2209205771356,19.824727767266,8.99742124475988));
#133302=CARTESIAN_POINT('Ctrl Pts',(-21.1982194166657,19.9102992971048,
9.00181942981815));
#133303=CARTESIAN_POINT('Ctrl Pts',(-21.1711995861977,19.9943633748381,
9.00621761487641));
#133304=CARTESIAN_POINT('Ctrl Pts',(-21.1441046030879,20.0786612674182,
9.01062803299537));
#133305=CARTESIAN_POINT('Ctrl Pts',(-21.1126670698914,20.1614429605725,
9.01503845111432));
#133306=CARTESIAN_POINT('Ctrl Pts',(-21.0770917883153,20.2422714829421,
9.01944886923327));
#133307=CARTESIAN_POINT('Ctrl Pts',(-21.0501146625114,20.3035646370618,
9.02279333761612));
#133308=CARTESIAN_POINT('Ctrl Pts',(-21.0207591774505,20.3637350853212,
9.02613780599898));
#133309=CARTESIAN_POINT('Ctrl Pts',(-20.989131617054,20.4226028184861,9.02948227438183));
#133310=CARTESIAN_POINT('Ctrl Pts',(-20.9495588772781,20.4962587519987,
9.03366690877488));
#133311=CARTESIAN_POINT('Ctrl Pts',(-20.9063001320242,20.5681109610611,
9.03785154316793));
#133312=CARTESIAN_POINT('Ctrl Pts',(-20.8595440286337,20.6377664778581,
9.04203617756098));
#133313=CARTESIAN_POINT('Ctrl Pts',(-20.8128544767691,20.7073228486487,
9.04621485564492));
#133314=CARTESIAN_POINT('Ctrl Pts',(-20.7626777089519,20.7746883591287,
9.05039353372887));
#133315=CARTESIAN_POINT('Ctrl Pts',(-20.7092482964898,20.8394944480145,
9.05457221181281));
#133316=CARTESIAN_POINT('Ctrl Pts',(-20.6548612002085,20.9054621394682,
9.05882578969825));
#133317=CARTESIAN_POINT('Ctrl Pts',(-20.5971039332158,20.9687773268415,
9.06307936758368));
#133318=CARTESIAN_POINT('Ctrl Pts',(-20.5362701954423,21.0290819955712,
9.06733294546912));
#133319=CARTESIAN_POINT('Ctrl Pts',(-20.4766158383828,21.0882175406228,
9.07150405944707));
#133320=CARTESIAN_POINT('Ctrl Pts',(-20.4140035745828,21.1444579161298,
9.07567517342502));
#133321=CARTESIAN_POINT('Ctrl Pts',(-20.3487498736145,21.1975001499275,
9.07984628740298));
#133322=CARTESIAN_POINT('Ctrl Pts',(-20.2835180691556,21.2505245848914,
9.08401600172335));
#133323=CARTESIAN_POINT('Ctrl Pts',(-20.2156469445306,21.3003527195436,
9.08818571604372));
#133324=CARTESIAN_POINT('Ctrl Pts',(-20.1454869304126,21.3467211066229,
9.0923554303641));
#133325=CARTESIAN_POINT('Ctrl Pts',(-20.0753294128889,21.3930878437159,
9.09652499630814));
#133326=CARTESIAN_POINT('Ctrl Pts',(-20.0028835520723,21.4359948250819,
9.10069456225219));
#133327=CARTESIAN_POINT('Ctrl Pts',(-19.92852856073,21.4752220557181,9.10486412819624));
#133328=CARTESIAN_POINT('Ctrl Pts',(-19.851559339619,21.5158284673914,9.10918029093516));
#133329=CARTESIAN_POINT('Ctrl Pts',(-19.7725447065604,21.5524913076845,
9.11349645367408));
#133330=CARTESIAN_POINT('Ctrl Pts',(-19.6919309796754,21.585019426664,9.117812616413));
#133331=CARTESIAN_POINT('Ctrl Pts',(-19.6139432364646,21.6164879455891,
9.12198818060468));
#133332=CARTESIAN_POINT('Ctrl Pts',(-19.5344594409714,21.6440868736177,
9.12616374479635));
#133333=CARTESIAN_POINT('Ctrl Pts',(-19.4539003149002,21.6676936187906,
9.13033930898803));
#133334=CARTESIAN_POINT('Ctrl Pts',(-19.3692723388823,21.6924926845425,
9.13472577100057));
#133335=CARTESIAN_POINT('Ctrl Pts',(-19.2834581156083,21.7128855434687,
9.13911223301312));
#133336=CARTESIAN_POINT('Ctrl Pts',(-19.1969566012277,21.7287909336122,
9.14349869502565));
#133337=CARTESIAN_POINT('Ctrl Pts',(-19.110455086847,21.7446963237556,9.14788515703819));
#133338=CARTESIAN_POINT('Ctrl Pts',(-19.0232668665414,21.756114245197,9.15227161905073));
#133339=CARTESIAN_POINT('Ctrl Pts',(-18.9358937423135,21.7630264334083,
9.15665808106326));
#133340=CARTESIAN_POINT('Ctrl Pts',(-18.8525407850492,21.7696205815937,
9.16084271545631));
#133341=CARTESIAN_POINT('Ctrl Pts',(-18.7687093097474,21.7721390606606,
9.16502734984936));
#133342=CARTESIAN_POINT('Ctrl Pts',(-18.68483185138,21.7705277871438,9.16921198424241));
#133343=CARTESIAN_POINT('Ctrl Pts',(-18.6010737821926,21.7689188070754,
9.17339066232635));
#133344=CARTESIAN_POINT('Ctrl Pts',(-18.5172703159603,21.7631917591217,
9.1775693404103));
#133345=CARTESIAN_POINT('Ctrl Pts',(-18.4338583233966,21.7533443853982,
9.18174801849424));
#133346=CARTESIAN_POINT('Ctrl Pts',(-18.3489512308133,21.7433205045778,
9.18600159637968));
#133347=CARTESIAN_POINT('Ctrl Pts',(-18.2644502649081,21.7290270933803,
9.19025517426511));
#133348=CARTESIAN_POINT('Ctrl Pts',(-18.1808154334733,21.7105173204754,
9.19450875215055));
#133349=CARTESIAN_POINT('Ctrl Pts',(-18.0988020264459,21.6923663956372,
9.1986798661285));
#133350=CARTESIAN_POINT('Ctrl Pts',(-18.0176219400175,21.6701612389658,
9.20285098010646));
#133351=CARTESIAN_POINT('Ctrl Pts',(-17.9377012248092,21.6440039582026,
9.20702209408441));
#133352=CARTESIAN_POINT('Ctrl Pts',(-17.8578073277689,21.6178554547676,
9.21119180840478));
#133353=CARTESIAN_POINT('Ctrl Pts',(-17.7791723995178,21.5877576040183,
9.21536152272516));
#133354=CARTESIAN_POINT('Ctrl Pts',(-17.7022076389883,21.5538624636879,
9.21953123704553));
#133355=CARTESIAN_POINT('Ctrl Pts',(-17.6252456171953,21.5199685294921,
9.22370080298958));
#133356=CARTESIAN_POINT('Ctrl Pts',(-17.549954065628,21.4822777605696,9.22787036893362));
#133357=CARTESIAN_POINT('Ctrl Pts',(-17.4767232259472,21.4409899357233,
9.23203993487766));
#133358=CARTESIAN_POINT('Ctrl Pts',(-17.4009176802832,21.3982504818895,
9.23635609761658));
#133359=CARTESIAN_POINT('Ctrl Pts',(-17.3273209113734,21.3516565799089,
9.24067226035551));
#133360=CARTESIAN_POINT('Ctrl Pts',(-17.2563352295955,21.3014800468565,
9.24498842309443));
#133361=CARTESIAN_POINT('Ctrl Pts',(-17.1876618989351,21.2529380090907,
9.24916398728611));
#133362=CARTESIAN_POINT('Ctrl Pts',(-17.121432497117,21.201043491951,9.25333955147779));
#133363=CARTESIAN_POINT('Ctrl Pts',(-17.0579778332573,21.146083899108,9.25751511566947));
#133364=CARTESIAN_POINT('Ctrl Pts',(-16.9913182251752,21.0883484278846,
9.26190157768201));
#133365=CARTESIAN_POINT('Ctrl Pts',(-16.9277214465954,21.027230514262,9.26628803969455));
#133366=CARTESIAN_POINT('Ctrl Pts',(-16.867525901464,20.9631057158443,9.27067450170709));
#133367=CARTESIAN_POINT('Ctrl Pts',(-16.8073303563327,20.8989809174267,
9.27506096371963));
#133368=CARTESIAN_POINT('Ctrl Pts',(-16.7505363613297,20.8318497263028,
9.27944742573217));
#133369=CARTESIAN_POINT('Ctrl Pts',(-16.6974308899393,20.7621241923026,
9.28383388774471));
#133370=CARTESIAN_POINT('Ctrl Pts',(-16.6467688800087,20.6956068334797,
9.28801852213775));
#133371=CARTESIAN_POINT('Ctrl Pts',(-16.5992748500802,20.6264810343216,
9.2922031565308));
#133372=CARTESIAN_POINT('Ctrl Pts',(-16.5552283987657,20.5550812139358,
9.29638779092385));
#133373=CARTESIAN_POINT('Ctrl Pts',(-16.5112446421229,20.4837830223567,
9.30056646900779));
#133374=CARTESIAN_POINT('Ctrl Pts',(-16.4706989563139,20.4102176270061,
9.30474514709174));
#133375=CARTESIAN_POINT('Ctrl Pts',(-16.4338297096935,20.3347511448677,
9.30892382517568));
#133376=CARTESIAN_POINT('Ctrl Pts',(-16.396299608325,20.2579319802738,9.31317740306112));
#133377=CARTESIAN_POINT('Ctrl Pts',(-16.3625793350038,20.17914328813,9.31743098094655));
#133378=CARTESIAN_POINT('Ctrl Pts',(-16.3328731767862,20.0988006413846,
9.32168455883199));
#133379=CARTESIAN_POINT('Ctrl Pts',(-16.3037429304124,20.0200155936222,
9.32585567280994));
#133380=CARTESIAN_POINT('Ctrl Pts',(-16.2784727120491,19.939736757811,9.33002678678789));
#133381=CARTESIAN_POINT('Ctrl Pts',(-16.2572072783656,19.8583776440833,
9.33419790076584));
#133382=CARTESIAN_POINT('Ctrl Pts',(-16.2359489805037,19.7770458311919,
9.33836761508621));
#133383=CARTESIAN_POINT('Ctrl Pts',(-16.2186929146628,19.6946349050202,
9.34253732940659));
#133384=CARTESIAN_POINT('Ctrl Pts',(-16.2055337985359,19.6115729247638,
9.34670704372696));
#133385=CARTESIAN_POINT('Ctrl Pts',(-16.1923751506668,19.528513900209,9.350876609671));
#133386=CARTESIAN_POINT('Ctrl Pts',(-16.1833132337911,19.4448043221315,
9.35504617561504));
#133387=CARTESIAN_POINT('Ctrl Pts',(-16.1783912959603,19.3608804584879,
9.35921574155909));
#133388=CARTESIAN_POINT('Ctrl Pts',(-16.1732963088673,19.2740059353298,
9.36353190429801));
#133389=CARTESIAN_POINT('Ctrl Pts',(-16.1726378716504,19.1869023041989,
9.36784806703693));
#133390=CARTESIAN_POINT('Ctrl Pts',(-16.1764051921425,19.1000549738833,
9.37216422977585));
#133391=CARTESIAN_POINT('Ctrl Pts',(-16.1800497925657,19.016036686218,9.37633979396753));
#133392=CARTESIAN_POINT('Ctrl Pts',(-16.1878361499306,18.9322587224488,
9.38051535815921));
#133393=CARTESIAN_POINT('Ctrl Pts',(-16.1997016639331,18.8491548068462,
9.38469092235089));
#133394=CARTESIAN_POINT('Ctrl Pts',(-16.2121664768403,18.7618535100274,
9.38907738436343));
#133395=CARTESIAN_POINT('Ctrl Pts',(-16.2291332400404,18.6752967161991,
9.39346384637597));
#133396=CARTESIAN_POINT('Ctrl Pts',(-16.2504693406595,18.5899722517346,
9.39785030838852));
#133397=CARTESIAN_POINT('Ctrl Pts',(-16.2718054412786,18.5046477872702,
9.40223677040106));
#133398=CARTESIAN_POINT('Ctrl Pts',(-16.2975106369606,18.4205561848056,
9.4066232324136));
#133399=CARTESIAN_POINT('Ctrl Pts',(-16.3273937923111,18.3381617783842,
9.41100969442614));
#133400=CARTESIAN_POINT('Ctrl Pts',(-16.3558995253308,18.2595652271093,
9.41519396859545));
#133401=CARTESIAN_POINT('Ctrl Pts',(-16.3883126378428,18.1822203306847,
9.41937824276476));
#133402=CARTESIAN_POINT('Ctrl Pts',(-16.4245033134286,18.1065430951298,
9.42356251693406));
#133403=CARTESIAN_POINT('Ctrl Pts',(-16.4606449439981,18.0309684161363,
9.42774112064292));
#133404=CARTESIAN_POINT('Ctrl Pts',(-16.5005537757522,17.9570573217751,
9.43191972435178));
#133405=CARTESIAN_POINT('Ctrl Pts',(-16.5440510006764,17.8852083948216,
9.43609832806064));
#133406=CARTESIAN_POINT('Ctrl Pts',(-16.5874980215117,17.8134423952254,
9.44027210886431));
#133407=CARTESIAN_POINT('Ctrl Pts',(-16.6345249665165,17.7437342236777,
9.44444588966797));
#133408=CARTESIAN_POINT('Ctrl Pts',(-16.6849066106035,17.6764589345568,
9.44861967047164));
#133409=CARTESIAN_POINT('Ctrl Pts',(-16.7352537172963,17.6092297636844,
9.45279059008417));
#133410=CARTESIAN_POINT('Ctrl Pts',(-16.7889506803249,17.5444305296909,
9.45696150969671));
#133411=CARTESIAN_POINT('Ctrl Pts',(-16.8457290001088,17.4824073264734,
9.46113242930925));
#133412=CARTESIAN_POINT('Ctrl Pts',(-16.9024956626441,17.4203968573399,
9.46530249258354));
#133413=CARTESIAN_POINT('Ctrl Pts',(-16.9623421216396,17.3611616320101,
9.46947255585784));
#133414=CARTESIAN_POINT('Ctrl Pts',(-17.0249603576165,17.3050137721479,
9.47364261913213));
#133415=CARTESIAN_POINT('Ctrl Pts',(-17.073202380668,17.2617566233716,9.47685529808206));
#133416=CARTESIAN_POINT('Ctrl Pts',(-17.1230887135075,17.2203313029939,
9.48006797703199));
#133417=CARTESIAN_POINT('Ctrl Pts',(-17.174464231106,17.180864983421,9.48328065598192));
#133418=CARTESIAN_POINT('Origin',(-18.734,19.211,-1.76670989022852));
#133419=CARTESIAN_POINT('',(-17.174464231106,17.180864983421,10.3499274761209));
#133420=CARTESIAN_POINT('',(-17.174464231106,17.180864983421,10.283238218494));
#133421=CARTESIAN_POINT('',(-17.174464231106,17.180864983421,-1.76670989022852));
#133422=CARTESIAN_POINT('',(-21.2939992159918,19.2089964727374,9.8332901097715));
#133423=CARTESIAN_POINT('Ctrl Pts',(-21.2939992159918,19.2089964727374,
9.8332901097715));
#133424=CARTESIAN_POINT('Ctrl Pts',(-21.2940649620946,19.2930033015151,
9.83745593779552));
#133425=CARTESIAN_POINT('Ctrl Pts',(-21.2899913508454,19.3770604200798,
9.84162176581953));
#133426=CARTESIAN_POINT('Ctrl Pts',(-21.281790209728,19.4607299485725,9.84578759384355));
#133427=CARTESIAN_POINT('Ctrl Pts',(-21.2735905258927,19.544384609609,9.84995268163075));
#133428=CARTESIAN_POINT('Ctrl Pts',(-21.2612648140692,19.6276513592372,
9.85411776941795));
#133429=CARTESIAN_POINT('Ctrl Pts',(-21.2448768408732,19.7100966739687,
9.85828285720515));
#133430=CARTESIAN_POINT('Ctrl Pts',(-21.2284868533627,19.7925521223993,
9.86244845694073));
#133431=CARTESIAN_POINT('Ctrl Pts',(-21.2080337038204,19.8741854840197,
9.86661405667632));
#133432=CARTESIAN_POINT('Ctrl Pts',(-21.183632148948,19.9545740278144,9.8707796564119));
#133433=CARTESIAN_POINT('Ctrl Pts',(-21.159203008195,20.0350534506039,9.87494996534483));
#133434=CARTESIAN_POINT('Ctrl Pts',(-21.1308166833999,20.114284804087,9.87912027427776));
#133435=CARTESIAN_POINT('Ctrl Pts',(-21.0986375209739,20.1918615572049,
9.88329058321069));
#133436=CARTESIAN_POINT('Ctrl Pts',(-21.066439637101,20.2694834435379,9.88746331837884));
#133437=CARTESIAN_POINT('Ctrl Pts',(-21.0304447198545,20.3454483968716,
9.89163605354698));
#133438=CARTESIAN_POINT('Ctrl Pts',(-20.9908638255709,20.4193731513193,
9.89580878871513));
#133439=CARTESIAN_POINT('Ctrl Pts',(-20.9512104382913,20.4934333000532,
9.89998916630974));
#133440=CARTESIAN_POINT('Ctrl Pts',(-20.907958193034,20.5654453913561,9.90416954390436));
#133441=CARTESIAN_POINT('Ctrl Pts',(-20.8613622504221,20.6350540212643,
9.90834992149897));
#133442=CARTESIAN_POINT('Ctrl Pts',(-20.8243993123263,20.6902721225411,
9.91166606942056));
#133443=CARTESIAN_POINT('Ctrl Pts',(-20.7853331875374,20.7439783287845,
9.91498221734216));
#133444=CARTESIAN_POINT('Ctrl Pts',(-20.7443085775785,20.7960108589263,
9.91829836526375));
#133445=CARTESIAN_POINT('Ctrl Pts',(-20.6925397790042,20.8616705099241,
9.9224829996568));
#133446=CARTESIAN_POINT('Ctrl Pts',(-20.6374544461771,20.9249134154189,
9.92666763404984));
#133447=CARTESIAN_POINT('Ctrl Pts',(-20.5793066365797,20.9853853631595,
9.93085226844289));
#133448=CARTESIAN_POINT('Ctrl Pts',(-20.5212415931921,21.0457712365674,
9.93503094652683));
#133449=CARTESIAN_POINT('Ctrl Pts',(-20.4601230476226,21.1033936577093,
9.93920962461076));
#133450=CARTESIAN_POINT('Ctrl Pts',(-20.3962460420505,21.1579304290825,
9.9433883026947));
#133451=CARTESIAN_POINT('Ctrl Pts',(-20.3312240870609,21.2134447328878,
9.94764188058014));
#133452=CARTESIAN_POINT('Ctrl Pts',(-20.2633441071063,21.2657612997089,
9.95189545846558));
#133453=CARTESIAN_POINT('Ctrl Pts',(-20.1929575410587,21.3145785921586,
9.95614903635102));
#133454=CARTESIAN_POINT('Ctrl Pts',(-20.1239355559419,21.3624494661351,
9.96032015032897));
#133455=CARTESIAN_POINT('Ctrl Pts',(-20.0525037029722,21.4069552612257,
9.96449126430692));
#133456=CARTESIAN_POINT('Ctrl Pts',(-19.979026280494,21.4478526015094,9.96866237828488));
#133457=CARTESIAN_POINT('Ctrl Pts',(-19.9055735140746,21.4887362182955,
9.97283209260525));
#133458=CARTESIAN_POINT('Ctrl Pts',(-19.8300769429976,21.5260135615003,
9.97700180692563));
#133459=CARTESIAN_POINT('Ctrl Pts',(-19.7529274425308,21.5594860797666,
9.981171521246));
#133460=CARTESIAN_POINT('Ctrl Pts',(-19.6757806873741,21.5929574069372,
9.98534108719005));
#133461=CARTESIAN_POINT('Ctrl Pts',(-19.5969815421365,21.6226239960434,
9.98951065313409));
#133462=CARTESIAN_POINT('Ctrl Pts',(-19.5169416763858,21.6483350880374,
9.99368021907814));
#133463=CARTESIAN_POINT('Ctrl Pts',(-19.4340877076953,21.6749501503077,
9.99799638181706));
#133464=CARTESIAN_POINT('Ctrl Pts',(-19.3499046498554,21.6973262283484,
10.002312544556));
#133465=CARTESIAN_POINT('Ctrl Pts',(-19.264865245119,21.7153526292287,10.0066287072949));
#133466=CARTESIAN_POINT('Ctrl Pts',(-19.1825959900472,21.7327918219964,
10.0108042714866));
#133467=CARTESIAN_POINT('Ctrl Pts',(-19.0995257948678,21.7461603390116,
10.0149798356783));
#133468=CARTESIAN_POINT('Ctrl Pts',(-19.0160902825553,21.7554105550182,
10.0191553998699));
#133469=CARTESIAN_POINT('Ctrl Pts',(-18.928440640865,21.7651279774449,10.0235418618825));
#133470=CARTESIAN_POINT('Ctrl Pts',(-18.840388390719,21.7703001003684,10.027928323895));
#133471=CARTESIAN_POINT('Ctrl Pts',(-18.7524390182804,21.7709335933975,
10.0323147859076));
#133472=CARTESIAN_POINT('Ctrl Pts',(-18.6644896458417,21.7715670864265,
10.0367012479201));
#133473=CARTESIAN_POINT('Ctrl Pts',(-18.576643727377,21.767662051318,10.0410877099326));
#133474=CARTESIAN_POINT('Ctrl Pts',(-18.4893986055751,21.759287691342,10.0454741719452));
#133475=CARTESIAN_POINT('Ctrl Pts',(-18.4061677611557,21.7512986480824,
10.0496588063382));
#133476=CARTESIAN_POINT('Ctrl Pts',(-18.3231738401582,21.7392127858656,
10.0538434407313));
#133477=CARTESIAN_POINT('Ctrl Pts',(-18.2408521955269,21.7230519984553,
10.0580280751243));
#133478=CARTESIAN_POINT('Ctrl Pts',(-18.1586477255675,21.7069142139257,
10.0622067532083));
#133479=CARTESIAN_POINT('Ctrl Pts',(-18.0771140788212,21.6867131129898,
10.0663854312922));
#133480=CARTESIAN_POINT('Ctrl Pts',(-17.9966818731345,21.6625223800316,
10.0705641093761));
#133481=CARTESIAN_POINT('Ctrl Pts',(-17.9148079779664,21.6378980455705,
10.0748176872616));
#133482=CARTESIAN_POINT('Ctrl Pts',(-17.8340758788423,21.6091396900265,
10.079071265147));
#133483=CARTESIAN_POINT('Ctrl Pts',(-17.7549293481812,21.5763796014059,
10.0833248430324));
#133484=CARTESIAN_POINT('Ctrl Pts',(-17.6773172274588,21.5442546310292,
10.0874959570104));
#133485=CARTESIAN_POINT('Ctrl Pts',(-17.6012301897821,21.5082818897809,
10.0916670709883));
#133486=CARTESIAN_POINT('Ctrl Pts',(-17.5270700635701,21.4686359601471,
10.0958381849663));
#133487=CARTESIAN_POINT('Ctrl Pts',(-17.4529348225046,21.4290033340878,
10.1000078992867));
#133488=CARTESIAN_POINT('Ctrl Pts',(-17.3807256141186,21.3857001842595,
10.104177613607));
#133489=CARTESIAN_POINT('Ctrl Pts',(-17.3108209620507,21.3389477028211,
10.1083473279274));
#133490=CARTESIAN_POINT('Ctrl Pts',(-17.2409187974905,21.2921968850367,
10.1125168938714));
#133491=CARTESIAN_POINT('Ctrl Pts',(-17.1733214081187,21.241997236139,10.1166864598155));
#133492=CARTESIAN_POINT('Ctrl Pts',(-17.1083783873658,21.1886133020731,
10.1208560257595));
#133493=CARTESIAN_POINT('Ctrl Pts',(-17.0411520501189,21.1333524547415,
10.1251721884984));
#133494=CARTESIAN_POINT('Ctrl Pts',(-16.976770617027,21.0746795720034,10.1294883512374));
#133495=CARTESIAN_POINT('Ctrl Pts',(-16.9155830497423,21.0129322392963,
10.1338045139763));
#133496=CARTESIAN_POINT('Ctrl Pts',(-16.8563886610263,20.9531963194576,
10.137980078168));
#133497=CARTESIAN_POINT('Ctrl Pts',(-16.8001835327305,20.8905835561615,
10.1421556423596));
#133498=CARTESIAN_POINT('Ctrl Pts',(-16.7472435046123,20.825434460743,10.1463312065513));
#133499=CARTESIAN_POINT('Ctrl Pts',(-16.6916296015266,20.756994839392,10.1507176685639));
#133500=CARTESIAN_POINT('Ctrl Pts',(-16.639619651693,20.6857564036312,10.1551041305764));
#133501=CARTESIAN_POINT('Ctrl Pts',(-16.5914816570987,20.6121477974616,
10.159490592589));
#133502=CARTESIAN_POINT('Ctrl Pts',(-16.5433436625044,20.538539191292,10.1638770546015));
#133503=CARTESIAN_POINT('Ctrl Pts',(-16.49907784951,20.4625609543416,10.1682635166141));
#133504=CARTESIAN_POINT('Ctrl Pts',(-16.4588952312818,20.3846687315233,
10.1726499786266));
#133505=CARTESIAN_POINT('Ctrl Pts',(-16.4205614748832,20.310360445341,10.1768346130197));
#133506=CARTESIAN_POINT('Ctrl Pts',(-16.3858007370466,20.2340338438632,
10.1810192474127));
#133507=CARTESIAN_POINT('Ctrl Pts',(-16.3548302568731,20.1560668406994,
10.1852038818058));
#133508=CARTESIAN_POINT('Ctrl Pts',(-16.3239038593448,20.0782108139142,
10.1893825598897));
#133509=CARTESIAN_POINT('Ctrl Pts',(-16.2967571717624,19.9987194471873,
10.1935612379737));
#133510=CARTESIAN_POINT('Ctrl Pts',(-16.273561322493,19.9179947059404,10.1977399160576));
#133511=CARTESIAN_POINT('Ctrl Pts',(-16.2499497042961,19.8358230317225,
10.201993493943));
#133512=CARTESIAN_POINT('Ctrl Pts',(-16.2304321761497,19.7523737600802,
10.2062470718285));
#133513=CARTESIAN_POINT('Ctrl Pts',(-16.2151377103691,19.6680916383782,
10.2105006497139));
#133514=CARTESIAN_POINT('Ctrl Pts',(-16.2001397576524,19.5854434900685,
10.2146717636919));
#133515=CARTESIAN_POINT('Ctrl Pts',(-16.189202669843,19.5019949698565,10.2188428776698));
#133516=CARTESIAN_POINT('Ctrl Pts',(-16.1823971528001,19.4181784500404,
10.2230139916478));
#133517=CARTESIAN_POINT('Ctrl Pts',(-16.1755939194141,19.3343900556669,
10.2271837059681));
#133518=CARTESIAN_POINT('Ctrl Pts',(-16.1729195406043,19.2502343650763,
10.2313534202885));
#133519=CARTESIAN_POINT('Ctrl Pts',(-16.1743929164357,19.1661493838666,
10.2355231346089));
#133520=CARTESIAN_POINT('Ctrl Pts',(-16.1758662398381,19.0820673947613,
10.2396927005529));
#133521=CARTESIAN_POINT('Ctrl Pts',(-16.1814870155134,18.9980565699815,
10.243862266497));
#133522=CARTESIAN_POINT('Ctrl Pts',(-16.1912220304804,18.9145540559805,
10.248031832441));
#133523=CARTESIAN_POINT('Ctrl Pts',(-16.2012993165642,18.8281156965988,
10.25234799518));
#133524=CARTESIAN_POINT('Ctrl Pts',(-16.2157854771197,18.7422225813443,
10.2566641579189));
#133525=CARTESIAN_POINT('Ctrl Pts',(-16.234585542542,18.657350860337,10.2609803206578));
#133526=CARTESIAN_POINT('Ctrl Pts',(-16.2527731978104,18.5752438267145,
10.2651558848495));
#133527=CARTESIAN_POINT('Ctrl Pts',(-16.2749978531259,18.4940931072449,
10.2693314490412));
#133528=CARTESIAN_POINT('Ctrl Pts',(-16.3011224991717,18.4143149518389,
10.2735070132328));
#133529=CARTESIAN_POINT('Ctrl Pts',(-16.3285666389838,18.3305073914578,
10.2778934752454));
#133530=CARTESIAN_POINT('Ctrl Pts',(-16.3603148903336,18.2482152402673,
10.2822799372579));
#133531=CARTESIAN_POINT('Ctrl Pts',(-16.3961518958431,18.1678958623944,
10.2866663992705));
#133532=CARTESIAN_POINT('Ctrl Pts',(-16.4319889013526,18.0875764845216,
10.291052861283));
#133533=CARTESIAN_POINT('Ctrl Pts',(-16.4719143298048,18.0092303623902,
10.2954393232955));
#133534=CARTESIAN_POINT('Ctrl Pts',(-16.5156592733601,17.9332815566289,
10.2998257853081));
#133535=CARTESIAN_POINT('Ctrl Pts',(-16.5573791055758,17.8608486952323,
10.3040091821606));
#133536=CARTESIAN_POINT('Ctrl Pts',(-16.6027278790349,17.7903265695032,
10.3081925790132));
#133537=CARTESIAN_POINT('Ctrl Pts',(-16.6515056001532,17.7221020603793,
10.3123759758657));
#133538=CARTESIAN_POINT('Ctrl Pts',(-16.7002227477591,17.6539622743228,
10.3165541776612));
#133539=CARTESIAN_POINT('Ctrl Pts',(-16.7523601281725,17.5881148134606,
10.3207323794568));
#133540=CARTESIAN_POINT('Ctrl Pts',(-16.8076724801956,17.5249210319667,
10.3249105812523));
#133541=CARTESIAN_POINT('Ctrl Pts',(-16.8629267561818,17.4617936017354,
10.329084396082));
#133542=CARTESIAN_POINT('Ctrl Pts',(-16.9213490806808,17.4013146604626,
10.3332582109116));
#133543=CARTESIAN_POINT('Ctrl Pts',(-16.9826524925986,17.3438144419156,
10.3374320257413));
#133544=CARTESIAN_POINT('Ctrl Pts',(-17.0438286406382,17.2864335919419,
10.3415971758678));
#133545=CARTESIAN_POINT('Ctrl Pts',(-17.1078736103551,17.2320194406792,
10.3457623259944));
#133546=CARTESIAN_POINT('Ctrl Pts',(-17.174464231106,17.180864983421,10.3499274761209));
#133547=CARTESIAN_POINT('Ctrl Pts',(-17.1725834074896,17.1783793283469,
9.54996332099649));
#133548=CARTESIAN_POINT('Ctrl Pts',(-17.7798204782461,16.7191701619952,
9.58795779796462));
#133549=CARTESIAN_POINT('Ctrl Pts',(-19.5298543890223,16.338845415249,9.66834421049323));
#133550=CARTESIAN_POINT('Ctrl Pts',(-21.1196060595483,17.7909993809188,
9.76278617061903));
#133551=CARTESIAN_POINT('Ctrl Pts',(-21.2937097337482,18.9257985538188,
9.81923365377672));
#133552=CARTESIAN_POINT('Ctrl Pts',(-21.2916489871171,19.2089800104295,
9.83328920137392));
#133553=CARTESIAN_POINT('',(-21.2939989766127,19.2132890482675,9.7667098901893));
#133554=CARTESIAN_POINT('Ctrl Pts',(-17.174464231106,17.180864983421,9.48328065598192));
#133555=CARTESIAN_POINT('Ctrl Pts',(-17.2411531716825,17.1296349975485,
9.48745093329683));
#133556=CARTESIAN_POINT('Ctrl Pts',(-17.3103521302254,17.0817075111554,
9.49162121061175));
#133557=CARTESIAN_POINT('Ctrl Pts',(-17.3816949027239,17.0373231786024,
9.49579148792666));
#133558=CARTESIAN_POINT('Ctrl Pts',(-17.4531170616135,16.992889457557,9.49996640570135));
#133559=CARTESIAN_POINT('Ctrl Pts',(-17.5266874037677,16.952007001496,9.50414132347604));
#133560=CARTESIAN_POINT('Ctrl Pts',(-17.602013491345,16.9148714007654,9.50831624125073));
#133561=CARTESIAN_POINT('Ctrl Pts',(-17.6773880098046,16.877711923713,9.51249384328738));
#133562=CARTESIAN_POINT('Ctrl Pts',(-17.7545200986259,16.8443042791516,
9.51667144532403));
#133563=CARTESIAN_POINT('Ctrl Pts',(-17.8329978366507,16.8147956886693,
9.52084904736067));
#133564=CARTESIAN_POINT('Ctrl Pts',(-17.9116031056638,16.7852391449737,
9.52503343824891));
#133565=CARTESIAN_POINT('Ctrl Pts',(-17.9915579506763,16.7595944403009,
9.52921782913714));
#133566=CARTESIAN_POINT('Ctrl Pts',(-18.072436301939,16.7379586591794,9.53340222002537));
#133567=CARTESIAN_POINT('Ctrl Pts',(-18.103254318857,16.7297145263771,9.53499664705277));
#133568=CARTESIAN_POINT('Ctrl Pts',(-18.1342063322878,16.7220519272115,
9.53659107408017));
#133569=CARTESIAN_POINT('Ctrl Pts',(-18.1652685194102,16.7149742583487,
9.53818550110756));
#133570=CARTESIAN_POINT('Ctrl Pts',(-18.2467924112676,16.6963986471497,
9.54237013550062));
#133571=CARTESIAN_POINT('Ctrl Pts',(-18.3293790330748,16.6817867038644,
9.54655476989366));
#133572=CARTESIAN_POINT('Ctrl Pts',(-18.4126082132396,16.6712544774323,
9.55073940428671));
#133573=CARTESIAN_POINT('Ctrl Pts',(-18.4957189269681,16.6607372423208,
9.55491808237065));
#133574=CARTESIAN_POINT('Ctrl Pts',(-18.5794699298767,16.654288246849,9.55909676045459));
#133575=CARTESIAN_POINT('Ctrl Pts',(-18.6634292675077,16.6519728857014,
9.56327543853853));
#133576=CARTESIAN_POINT('Ctrl Pts',(-18.7488935159254,16.6496160233692,
9.56752901642397));
#133577=CARTESIAN_POINT('Ctrl Pts',(-18.8345731712375,16.6515425508617,
9.57178259430941));
#133578=CARTESIAN_POINT('Ctrl Pts',(-18.9200053717023,16.6577663636679,
9.57603617219484));
#133579=CARTESIAN_POINT('Ctrl Pts',(-19.0037813022539,16.663869515718,9.5802072861728));
#133580=CARTESIAN_POINT('Ctrl Pts',(-19.0873188071791,16.6741047825048,
9.58437840015075));
#133581=CARTESIAN_POINT('Ctrl Pts',(-19.1701815497895,16.6884327252533,
9.5885495141287));
#133582=CARTESIAN_POINT('Ctrl Pts',(-19.2530164870063,16.7027558601221,
9.59271922844908));
#133583=CARTESIAN_POINT('Ctrl Pts',(-19.3351766586591,16.7211688651668,
9.59688894276945));
#133584=CARTESIAN_POINT('Ctrl Pts',(-19.4162332022014,16.7435807292205,
9.60105865708982));
#133585=CARTESIAN_POINT('Ctrl Pts',(-19.4972868614039,16.7659917957639,
9.60522822303387));
#133586=CARTESIAN_POINT('Ctrl Pts',(-19.5772365274095,16.7924013149753,
9.60939778897792));
#133587=CARTESIAN_POINT('Ctrl Pts',(-19.6556671754964,16.8226680260876,
9.61356735492196));
#133588=CARTESIAN_POINT('Ctrl Pts',(-19.7368553484154,16.8539988774245,
9.61788351766088));
#133589=CARTESIAN_POINT('Ctrl Pts',(-19.8164152065818,16.8894630151456,
9.6221996803998));
#133590=CARTESIAN_POINT('Ctrl Pts',(-19.8939093684295,16.9288496418883,
9.62651584313872));
#133591=CARTESIAN_POINT('Ctrl Pts',(-19.9688791661059,16.9669532534076,
9.6306914073304));
#133592=CARTESIAN_POINT('Ctrl Pts',(-20.0419153954164,17.0087274533692,
9.63486697152208));
#133593=CARTESIAN_POINT('Ctrl Pts',(-20.112649171425,17.0539356842855,9.63904253571376));
#133594=CARTESIAN_POINT('Ctrl Pts',(-20.1869555423063,17.1014272754729,
9.6434289977263));
#133595=CARTESIAN_POINT('Ctrl Pts',(-20.2587202783153,17.1527085808079,
9.64781545973885));
#133596=CARTESIAN_POINT('Ctrl Pts',(-20.3275542346358,17.2074569130477,
9.65220192175139));
#133597=CARTESIAN_POINT('Ctrl Pts',(-20.3963881909563,17.2622052452876,
9.65658838376393));
#133598=CARTESIAN_POINT('Ctrl Pts',(-20.4622909830917,17.3204201632972,
9.66097484577647));
#133599=CARTESIAN_POINT('Ctrl Pts',(-20.5249190804939,17.3817354354487,
9.66536130778901));
#133600=CARTESIAN_POINT('Ctrl Pts',(-20.5852113014986,17.440763796406,9.66958416538902));
#133601=CARTESIAN_POINT('Ctrl Pts',(-20.6427127908696,17.5029045422552,
9.67380702298903));
#133602=CARTESIAN_POINT('Ctrl Pts',(-20.6970796830689,17.5678572314245,
9.67802988058905));
#133603=CARTESIAN_POINT('Ctrl Pts',(-20.7500936846377,17.6311936081461,
9.68214765466765));
#133604=CARTESIAN_POINT('Ctrl Pts',(-20.8001269202378,17.697203245602,9.68626542874624));
#133605=CARTESIAN_POINT('Ctrl Pts',(-20.8468954124061,17.7655682388181,
9.69038320282484));
#133606=CARTESIAN_POINT('Ctrl Pts',(-20.89361966769,17.8338685676809,9.69449708202705));
#133607=CARTESIAN_POINT('Ctrl Pts',(-20.9370850392269,17.9045194435154,
9.69861096122926));
#133608=CARTESIAN_POINT('Ctrl Pts',(-20.9770478427322,17.9771700379653,
9.70272484043147));
#133609=CARTESIAN_POINT('Ctrl Pts',(-21.016985643432,18.0497751784301,9.70683614577719));
#133610=CARTESIAN_POINT('Ctrl Pts',(-21.0534249974544,18.1243771397533,
9.71094745112291));
#133611=CARTESIAN_POINT('Ctrl Pts',(-21.0861664418209,18.2005975900803,
9.71505875646863));
#133612=CARTESIAN_POINT('Ctrl Pts',(-21.1204445396303,18.2803952930204,
9.71936301761202));
#133613=CARTESIAN_POINT('Ctrl Pts',(-21.1506688210159,18.3619666588744,
9.72366727875541));
#133614=CARTESIAN_POINT('Ctrl Pts',(-21.1766659614561,18.4448518415192,
9.7279715398988));
#133615=CARTESIAN_POINT('Ctrl Pts',(-21.2014998963996,18.5240284432037,
9.73208321292915));
#133616=CARTESIAN_POINT('Ctrl Pts',(-21.2224767553181,18.6044033134951,
9.7361948859595));
#133617=CARTESIAN_POINT('Ctrl Pts',(-21.2394965458158,18.6855601281733,
9.74030655898986));
#133618=CARTESIAN_POINT('Ctrl Pts',(-21.2565208804897,18.7667386112071,
9.74441932981087));
#133619=CARTESIAN_POINT('Ctrl Pts',(-21.2695859645565,18.8486989864203,
9.74853210063189));
#133620=CARTESIAN_POINT('Ctrl Pts',(-21.2786432445869,18.9310165044542,
9.7526448714529));
#133621=CARTESIAN_POINT('Ctrl Pts',(-21.2877094512627,19.0134151527261,
9.75676169572553));
#133622=CARTESIAN_POINT('Ctrl Pts',(-21.2927599450141,19.0961711731438,
9.76087851999816));
#133623=CARTESIAN_POINT('Ctrl Pts',(-21.2937982075177,19.1788575547119,
9.76499534427079));
#133624=CARTESIAN_POINT('Ctrl Pts',(-21.2939423435977,19.1903364349236,
9.76556685957696));
#133625=CARTESIAN_POINT('Ctrl Pts',(-21.2940092371596,19.2018139780893,
9.76613837488313));
#133626=CARTESIAN_POINT('Ctrl Pts',(-21.2939989766127,19.2132890482674,
9.7667098901893));
#133627=CARTESIAN_POINT('Ctrl Pts',(-21.293998976612,19.2132890490549,9.76670989022852));
#133628=CARTESIAN_POINT('Ctrl Pts',(-21.2938920610985,19.3328599270272,
9.77266511192853));
#133629=CARTESIAN_POINT('Ctrl Pts',(-21.2854044483393,19.4520702292311,
9.77862033362855));
#133630=CARTESIAN_POINT('Ctrl Pts',(-21.2687069780215,19.5699714968758,
9.78457555532857));
#133631=CARTESIAN_POINT('Ctrl Pts',(-21.2612660069347,19.6225123852221,
9.78722940837586));
#133632=CARTESIAN_POINT('Ctrl Pts',(-21.2521952261605,19.6747937484515,
9.78988326142315));
#133633=CARTESIAN_POINT('Ctrl Pts',(-21.2415125421986,19.7267333135613,
9.79253711447044));
#133634=CARTESIAN_POINT('Ctrl Pts',(-21.2246679295087,19.8086323813113,
9.79672174886349));
#133635=CARTESIAN_POINT('Ctrl Pts',(-21.2037753333228,19.8898577370366,
9.80090638325654));
#133636=CARTESIAN_POINT('Ctrl Pts',(-21.1789030820534,19.9699788662181,
9.80509101764959));
#133637=CARTESIAN_POINT('Ctrl Pts',(-21.154066233355,20.0499859528893,9.80926969573354));
#133638=CARTESIAN_POINT('Ctrl Pts',(-21.125261116367,20.1288914993745,9.81344837381749));
#133639=CARTESIAN_POINT('Ctrl Pts',(-21.0926070466711,20.2062752380087,
9.81762705190143));
#133640=CARTESIAN_POINT('Ctrl Pts',(-21.0593676762441,20.2850460245431,
9.82188062978687));
#133641=CARTESIAN_POINT('Ctrl Pts',(-21.022140108072,20.362239437543,9.8261342076723));
#133642=CARTESIAN_POINT('Ctrl Pts',(-20.9811033321017,20.4374283977703,
9.83038778555774));
#133643=CARTESIAN_POINT('Ctrl Pts',(-20.9408621341102,20.5111596732845,
9.83455889953569));
#133644=CARTESIAN_POINT('Ctrl Pts',(-20.8969583386824,20.5829631005171,
9.83873001351364));
#133645=CARTESIAN_POINT('Ctrl Pts',(-20.8496085018329,20.6524578269836,
9.84290112749159));
#133646=CARTESIAN_POINT('Ctrl Pts',(-20.8022745536785,20.7219292338234,
9.84707084181197));
#133647=CARTESIAN_POINT('Ctrl Pts',(-20.7514971194517,20.7890930986179,
9.85124055613234));
#133648=CARTESIAN_POINT('Ctrl Pts',(-20.6975366051101,20.853596724821,9.85541027045272));
#133649=CARTESIAN_POINT('Ctrl Pts',(-20.643578010915,20.9180980557084,9.85957983639676));
#133650=CARTESIAN_POINT('Ctrl Pts',(-20.5864368576391,20.9799389839169,
9.86374940234081));
#133651=CARTESIAN_POINT('Ctrl Pts',(-20.5264135623405,21.0388002137919,
9.86791896828486));
#133652=CARTESIAN_POINT('Ctrl Pts',(-20.4642799220261,21.099730931896,9.87223513102378));
#133653=CARTESIAN_POINT('Ctrl Pts',(-20.3990580731255,21.1574681514492,
9.87655129376269));
#133654=CARTESIAN_POINT('Ctrl Pts',(-20.3311209857105,21.2117010163947,
9.88086745650161));
#133655=CARTESIAN_POINT('Ctrl Pts',(-20.2653969417723,21.264167251469,9.88504302069329));
#133656=CARTESIAN_POINT('Ctrl Pts',(-20.1971322502975,21.3133536974901,
9.88921858488498));
#133657=CARTESIAN_POINT('Ctrl Pts',(-20.1266949702183,21.3590225138319,
9.89339414907666));
#133658=CARTESIAN_POINT('Ctrl Pts',(-20.0527000705711,21.4069979535197,
9.89778061108919));
#133659=CARTESIAN_POINT('Ctrl Pts',(-19.9763078452047,21.4510907819034,
9.90216707310173));
#133660=CARTESIAN_POINT('Ctrl Pts',(-19.8979731420051,21.4910803768049,
9.90655353511427));
#133661=CARTESIAN_POINT('Ctrl Pts',(-19.8196384388055,21.5310699717064,
9.91093999712681));
#133662=CARTESIAN_POINT('Ctrl Pts',(-19.7393618185147,21.5669561657756,
9.91532645913934));
#133663=CARTESIAN_POINT('Ctrl Pts',(-19.6576188802167,21.5985778865007,
9.91971292115187));
#133664=CARTESIAN_POINT('Ctrl Pts',(-19.5796370556819,21.6287446449807,
9.92389755554492));
#133665=CARTESIAN_POINT('Ctrl Pts',(-19.5000306196521,21.6551430224068,
9.92808218993797));
#133666=CARTESIAN_POINT('Ctrl Pts',(-19.4191985515815,21.6775974428168,
9.93226682433101));
#133667=CARTESIAN_POINT('Ctrl Pts',(-19.3384815379547,21.7000199021387,
9.93644550241496));
#133668=CARTESIAN_POINT('Ctrl Pts',(-19.2565427969408,21.7185094330108,
9.9406241804989));
#133669=CARTESIAN_POINT('Ctrl Pts',(-19.1738002903986,21.7329388780391,
9.94480285858285));
#133670=CARTESIAN_POINT('Ctrl Pts',(-19.0895746838927,21.7476269604994,
9.94905643646829));
#133671=CARTESIAN_POINT('Ctrl Pts',(-19.0045166631074,21.758107797425,9.95331001435372));
#133672=CARTESIAN_POINT('Ctrl Pts',(-18.9190822179584,21.7643007211442,
9.95756359223916));
#133673=CARTESIAN_POINT('Ctrl Pts',(-18.8353040862403,21.7703735829526,
9.96173470621711));
#133674=CARTESIAN_POINT('Ctrl Pts',(-18.7511644753126,21.7723232722254,
9.96590582019506));
#133675=CARTESIAN_POINT('Ctrl Pts',(-18.6671008395073,21.7701257300737,
9.97007693417301));
#133676=CARTESIAN_POINT('Ctrl Pts',(-18.5830654120668,21.7679289253285,
9.97424664849338));
#133677=CARTESIAN_POINT('Ctrl Pts',(-18.49910636861,21.7615876649968,9.97841636281376));
#133678=CARTESIAN_POINT('Ctrl Pts',(-18.4156612239222,21.7511300013277,
9.98258607713413));
#133679=CARTESIAN_POINT('Ctrl Pts',(-18.3322190485708,21.7406727097872,
9.98675564307818));
#133680=CARTESIAN_POINT('Ctrl Pts',(-18.2492911919861,21.7260993641991,
9.99092520902222));
#133681=CARTESIAN_POINT('Ctrl Pts',(-18.1673087413395,21.7074897390852,
9.99509477496626));
#133682=CARTESIAN_POINT('Ctrl Pts',(-18.0824438888645,21.6882258225098,
9.99941093770518));
#133683=CARTESIAN_POINT('Ctrl Pts',(-17.9985926745536,21.664636631037,10.0037271004441));
#133684=CARTESIAN_POINT('Ctrl Pts',(-17.9162183607824,21.6368675129855,
10.008043263183));
#133685=CARTESIAN_POINT('Ctrl Pts',(-17.8365273816181,21.6100029710338,
10.0122188273747));
#133686=CARTESIAN_POINT('Ctrl Pts',(-17.7582189816851,21.5792268589616,
10.0163943915664));
#133687=CARTESIAN_POINT('Ctrl Pts',(-17.6816923706303,21.5447199174645,
10.0205699557581));
#133688=CARTESIAN_POINT('Ctrl Pts',(-17.601300582376,21.5084701123847,10.0249564177706));
#133689=CARTESIAN_POINT('Ctrl Pts',(-17.5228758288489,21.4681029519008,
10.0293428797831));
#133690=CARTESIAN_POINT('Ctrl Pts',(-17.4468498189205,21.423881472503,10.0337293417957));
#133691=CARTESIAN_POINT('Ctrl Pts',(-17.3708238089921,21.3796599931052,
10.0381158038082));
#133692=CARTESIAN_POINT('Ctrl Pts',(-17.2971969868962,21.3315845757053,
10.0425022658208));
#133693=CARTESIAN_POINT('Ctrl Pts',(-17.2263622218889,21.2799679383722,
10.0468887278333));
#133694=CARTESIAN_POINT('Ctrl Pts',(-17.1587866694218,21.230726259037,10.0510733622264));
#133695=CARTESIAN_POINT('Ctrl Pts',(-17.0935003576728,21.1780787853436,
10.0552579966194));
#133696=CARTESIAN_POINT('Ctrl Pts',(-17.0308668782518,21.1222659599345,
10.0594426310125));
#133697=CARTESIAN_POINT('Ctrl Pts',(-16.9683225498363,21.0665325771741,
10.0636213090964));
#133698=CARTESIAN_POINT('Ctrl Pts',(-16.908423893985,21.0076430954477,10.0677999871803));
#133699=CARTESIAN_POINT('Ctrl Pts',(-16.8515040647698,20.9458801266491,
10.0719786652643));
#133700=CARTESIAN_POINT('Ctrl Pts',(-16.7935639885235,20.883010101023,10.0762322431497));
#133701=CARTESIAN_POINT('Ctrl Pts',(-16.7387109698993,20.8171628445092,
10.0804858210352));
#133702=CARTESIAN_POINT('Ctrl Pts',(-16.6872596563362,20.7486781085841,
10.0847393989206));
#133703=CARTESIAN_POINT('Ctrl Pts',(-16.6368058268854,20.6815210829019,
10.0889105128986));
#133704=CARTESIAN_POINT('Ctrl Pts',(-16.5896232711908,20.6118283153184,
10.0930816268765));
#133705=CARTESIAN_POINT('Ctrl Pts',(-16.5459690047033,20.5399546130779,
10.0972527408545));
#133706=CARTESIAN_POINT('Ctrl Pts',(-16.5023293868266,20.4681050287523,
10.1014224551748));
#133707=CARTESIAN_POINT('Ctrl Pts',(-16.4622159454254,20.3940763560657,
10.1055921694952));
#133708=CARTESIAN_POINT('Ctrl Pts',(-16.4258419114527,20.318251659865,10.1097618838156));
#133709=CARTESIAN_POINT('Ctrl Pts',(-16.3894691718243,20.2424296618324,
10.1139314497596));
#133710=CARTESIAN_POINT('Ctrl Pts',(-16.3568357732639,20.1648121825009,
10.1181010157037));
#133711=CARTESIAN_POINT('Ctrl Pts',(-16.3281079773328,20.0858048783966,
10.1222705816477));
#133712=CARTESIAN_POINT('Ctrl Pts',(-16.2983701475364,20.004019774946,10.1265867443866));
#133713=CARTESIAN_POINT('Ctrl Pts',(-16.2728178525521,19.920745791513,10.1309029071256));
#133714=CARTESIAN_POINT('Ctrl Pts',(-16.2515796325832,19.8364511327309,
10.1352190698645));
#133715=CARTESIAN_POINT('Ctrl Pts',(-16.231033245396,19.7549023635925,10.1393946340562));
#133716=CARTESIAN_POINT('Ctrl Pts',(-16.2145242335759,19.6723988660723,
10.1435701982478));
#133717=CARTESIAN_POINT('Ctrl Pts',(-16.2021167074112,19.5893741438175,
10.1477457624395));
#133718=CARTESIAN_POINT('Ctrl Pts',(-16.189082506596,19.5021560402142,10.1521322244521));
#133719=CARTESIAN_POINT('Ctrl Pts',(-16.1805750686802,19.414363255138,10.1565186864646));
#133720=CARTESIAN_POINT('Ctrl Pts',(-16.176606897426,19.3265011640937,10.1609051484772));
#133721=CARTESIAN_POINT('Ctrl Pts',(-16.1726387261718,19.2386390730495,
10.1652916104897));
#133722=CARTESIAN_POINT('Ctrl Pts',(-16.173209741748,19.1507082557479,10.1696780725022));
#133723=CARTESIAN_POINT('Ctrl Pts',(-16.1782696504243,19.0632083214198,
10.1740645345148));
#133724=CARTESIAN_POINT('Ctrl Pts',(-16.1830972264457,18.9797260667259,
10.1782495861008));
#133725=CARTESIAN_POINT('Ctrl Pts',(-16.1920284781124,18.8963252255056,
10.1824346376868));
#133726=CARTESIAN_POINT('Ctrl Pts',(-16.2050580322512,18.8134417982748,
10.1866196892728));
#133727=CARTESIAN_POINT('Ctrl Pts',(-16.2180651804963,18.7307008991188,
10.1907975441566));
#133728=CARTESIAN_POINT('Ctrl Pts',(-16.2351565463974,18.6484760952712,
10.1949753990404));
#133729=CARTESIAN_POINT('Ctrl Pts',(-16.2562748618428,18.5672002331905,
10.1991532539242));
#133730=CARTESIAN_POINT('Ctrl Pts',(-16.2773725113752,18.4860039058583,
10.2033270204522));
#133731=CARTESIAN_POINT('Ctrl Pts',(-16.3024891716603,18.4057551192321,
10.2075007869803));
#133732=CARTESIAN_POINT('Ctrl Pts',(-16.3315163412326,18.326877684166,10.2116745535083));
#133733=CARTESIAN_POINT('Ctrl Pts',(-16.3605238139034,18.2480537727846,
10.215845487853));
#133734=CARTESIAN_POINT('Ctrl Pts',(-16.3934363671985,18.1705997951908,
10.2200164221976));
#133735=CARTESIAN_POINT('Ctrl Pts',(-16.4300957454762,18.0949242024006,
10.2241873565423));
#133736=CARTESIAN_POINT('Ctrl Pts',(-16.4667412452109,18.0192772589498,
10.2283567118505));
#133737=CARTESIAN_POINT('Ctrl Pts',(-16.5071305503789,17.9454077756885,
10.2325260671588));
#133738=CARTESIAN_POINT('Ctrl Pts',(-16.5510579279904,17.8737027592003,
10.236695422467));
#133739=CARTESIAN_POINT('Ctrl Pts',(-16.5950001276849,17.8019735478304,
10.2408661846093));
#133740=CARTESIAN_POINT('Ctrl Pts',(-16.6424825512063,17.7324106591257,
10.2450369467516));
#133741=CARTESIAN_POINT('Ctrl Pts',(-16.6932547035781,17.6653743547897,
10.2492077088939));
#133742=CARTESIAN_POINT('Ctrl Pts',(-16.7440345633082,17.5983278741504,
10.2533791041699));
#133743=CARTESIAN_POINT('Ctrl Pts',(-16.7981048586349,17.5338091011393,
10.2575504994459));
#133744=CARTESIAN_POINT('Ctrl Pts',(-16.8551743954097,17.4721456796109,
10.2617218947218));
#133745=CARTESIAN_POINT('Ctrl Pts',(-16.9123064332965,17.4104147258642,
10.2658978584043));
#133746=CARTESIAN_POINT('Ctrl Pts',(-16.9724439505659,17.3515456983761,
10.2700738220868));
#133747=CARTESIAN_POINT('Ctrl Pts',(-17.0352588293081,17.2958293979397,
10.2742497857693));
#133748=CARTESIAN_POINT('Ctrl Pts',(-17.0803268546882,17.2558544160176,
10.2772459300109));
#133749=CARTESIAN_POINT('Ctrl Pts',(-17.126772332044,17.2175015725475,10.2802420742524));
#133750=CARTESIAN_POINT('Ctrl Pts',(-17.174464231106,17.180864983421,10.283238218494));
#133751=CARTESIAN_POINT('Origin',(-18.734,19.211,-1.76670989022852));
#133752=CARTESIAN_POINT('',(-17.1757181102512,17.1824653653531,11.1497835165008));
#133753=CARTESIAN_POINT('',(-17.1731949711369,17.1791828613964,11.0834063356124));
#133754=CARTESIAN_POINT('',(-17.174464231106,17.180864983421,-1.76670989022852));
#133755=CARTESIAN_POINT('',(-21.2939995125392,19.2125798097912,10.6332901097715));
#133756=CARTESIAN_POINT('Ctrl Pts',(-21.2907953051338,19.2125971079063,
10.6332910656997));
#133757=CARTESIAN_POINT('Ctrl Pts',(-21.292607272731,19.5356421908361,10.6493117789173));
#133758=CARTESIAN_POINT('Ctrl Pts',(-21.0857646549701,20.7112479426697,
10.7077244276952));
#133759=CARTESIAN_POINT('Ctrl Pts',(-19.318984802206,22.1810310672293,10.8085290120338));
#133760=CARTESIAN_POINT('Ctrl Pts',(-16.5533150683864,21.3105011284,10.9357048187152));
#133761=CARTESIAN_POINT('Ctrl Pts',(-15.8690423811832,18.8090198107934,
11.0494563202042));
#133762=CARTESIAN_POINT('Ctrl Pts',(-16.7160809400405,17.5418442729995,
11.1208158861327));
#133763=CARTESIAN_POINT('Ctrl Pts',(-17.175718110251,17.1824653653533,11.1497835165008));
#133764=CARTESIAN_POINT('Ctrl Pts',(-17.174464231106,17.180864983421,10.3499274761209));
#133765=CARTESIAN_POINT('Ctrl Pts',(-17.2411280860223,17.1296542681803,
10.354097206942));
#133766=CARTESIAN_POINT('Ctrl Pts',(-17.3103428504281,17.0817107249359,
10.3582669377631));
#133767=CARTESIAN_POINT('Ctrl Pts',(-17.3817510958368,17.0372882203039,
10.3624366685842));
#133768=CARTESIAN_POINT('Ctrl Pts',(-17.4531563510901,16.992867575824,10.3666062248017));
#133769=CARTESIAN_POINT('Ctrl Pts',(-17.5267545137001,16.9519679191462,
10.3707757810191));
#133770=CARTESIAN_POINT('Ctrl Pts',(-17.6021605539753,16.9147989050559,
10.3749453372365));
#133771=CARTESIAN_POINT('Ctrl Pts',(-17.6806132684811,16.8761281296082,
10.3792833584659));
#133772=CARTESIAN_POINT('Ctrl Pts',(-17.7610225775555,16.8414961150588,
10.3836213796953));
#133773=CARTESIAN_POINT('Ctrl Pts',(-17.842930188215,16.8110844617934,10.3879594009247));
#133774=CARTESIAN_POINT('Ctrl Pts',(-17.9217696726806,16.7818119797141,
10.3921349269177));
#133775=CARTESIAN_POINT('Ctrl Pts',(-18.0019967422928,16.7564494038124,
10.3963104529106));
#133776=CARTESIAN_POINT('Ctrl Pts',(-18.0831874283277,16.7351076363151,
10.4004859789035));
#133777=CARTESIAN_POINT('Ctrl Pts',(-18.1644361653549,16.7137506095455,
10.4046644903796));
#133778=CARTESIAN_POINT('Ctrl Pts',(-18.2466494404615,16.6964202058467,
10.4088430018557));
#133779=CARTESIAN_POINT('Ctrl Pts',(-18.329394229314,16.6831760009195,10.4130215133318));
#133780=CARTESIAN_POINT('Ctrl Pts',(-18.4122672488332,16.669911271277,10.4172065003011));
#133781=CARTESIAN_POINT('Ctrl Pts',(-18.4956729694358,16.660745419148,10.4213914872703));
#133782=CARTESIAN_POINT('Ctrl Pts',(-18.5791750874247,16.6556860767323,
10.4255764742396));
#133783=CARTESIAN_POINT('Ctrl Pts',(-18.5886534403544,16.6551117891074,
10.4260515134895));
#133784=CARTESIAN_POINT('Ctrl Pts',(-18.5981330383419,16.6545903570305,
10.4265265527395));
#133785=CARTESIAN_POINT('Ctrl Pts',(-18.6076132463769,16.6541217493771,
10.4270015919895));
#133786=CARTESIAN_POINT('Ctrl Pts',(-18.6911246711662,16.6499937711024,
10.4311862263825));
#133787=CARTESIAN_POINT('Ctrl Pts',(-18.7749939587051,16.6499538232249,
10.4353708607756));
#133788=CARTESIAN_POINT('Ctrl Pts',(-18.8587871646375,16.6540431830902,
10.4395554951686));
#133789=CARTESIAN_POINT('Ctrl Pts',(-18.9424611013131,16.6581267222578,
10.4437341732526));
#133790=CARTESIAN_POINT('Ctrl Pts',(-19.0260587159297,16.666327872255,10.4479128513366));
#133791=CARTESIAN_POINT('Ctrl Pts',(-19.1091432618604,16.6786359793504,
10.4520915294205));
#133792=CARTESIAN_POINT('Ctrl Pts',(-19.1937170385645,16.6911647004197,
10.456345107306));
#133793=CARTESIAN_POINT('Ctrl Pts',(-19.2777586906013,16.707949084993,10.4605986851914));
#133794=CARTESIAN_POINT('Ctrl Pts',(-19.3608099823644,16.7289223932342,
10.4648522630768));
#133795=CARTESIAN_POINT('Ctrl Pts',(-19.4422511627754,16.7494890929691,
10.4690233770548));
#133796=CARTESIAN_POINT('Ctrl Pts',(-19.5227395737981,16.774083627044,10.4731944910327));
#133797=CARTESIAN_POINT('Ctrl Pts',(-19.6018523684388,16.8025913414466,
10.4773656050107));
#133798=CARTESIAN_POINT('Ctrl Pts',(-19.6809386160173,16.8310894898103,
10.481535319331));
#133799=CARTESIAN_POINT('Ctrl Pts',(-19.7586497315296,16.8634980548298,
10.4857050336514));
#133800=CARTESIAN_POINT('Ctrl Pts',(-19.8345791893321,16.8996528932224,
10.4898747479718));
#133801=CARTESIAN_POINT('Ctrl Pts',(-19.9105059452388,16.9358064450708,
10.4940443139158));
#133802=CARTESIAN_POINT('Ctrl Pts',(-19.9846507545057,16.9757058066968,
10.4982138798599));
#133803=CARTESIAN_POINT('Ctrl Pts',(-20.0566294498852,17.0191397539313,
10.5023834458039));
#133804=CARTESIAN_POINT('Ctrl Pts',(-20.1311388273987,17.0641007851689,
10.5066996085429));
#133805=CARTESIAN_POINT('Ctrl Pts',(-20.2033264842393,17.112849306127,10.5110157712818));
#133806=CARTESIAN_POINT('Ctrl Pts',(-20.2727983186256,17.1651017291676,
10.5153319340207));
#133807=CARTESIAN_POINT('Ctrl Pts',(-20.340007115314,17.2156520350236,10.5195074982124));
#133808=CARTESIAN_POINT('Ctrl Pts',(-20.40467397639,17.2694811317362,10.523683062404));
#133809=CARTESIAN_POINT('Ctrl Pts',(-20.4664767307277,17.3262919649221,
10.5278586265957));
#133810=CARTESIAN_POINT('Ctrl Pts',(-20.5314009952648,17.3859721782373,
10.5322450886082));
#133811=CARTESIAN_POINT('Ctrl Pts',(-20.5931638083647,17.4489428422743,
10.5366315506208));
#133812=CARTESIAN_POINT('Ctrl Pts',(-20.6514380125592,17.5148185627731,
10.5410180126333));
#133813=CARTESIAN_POINT('Ctrl Pts',(-20.7097122167537,17.580694283272,10.5454044746458));
#133814=CARTESIAN_POINT('Ctrl Pts',(-20.7644975100435,17.649474559,10.5497909366584));
#133815=CARTESIAN_POINT('Ctrl Pts',(-20.8155192213964,17.7207390393097,
10.5541773986709));
#133816=CARTESIAN_POINT('Ctrl Pts',(-20.8646271615162,17.789330463214,10.5583993290636));
#133817=CARTESIAN_POINT('Ctrl Pts',(-20.91043082465,17.8604769154309,10.5626212594563));
#133818=CARTESIAN_POINT('Ctrl Pts',(-20.9526566798058,17.9338302629825,
10.5668431898491));
#133819=CARTESIAN_POINT('Ctrl Pts',(-20.9948201353165,18.0070752119515,
10.5710588812454));
#133820=CARTESIAN_POINT('Ctrl Pts',(-21.0334160638336,18.0825201920568,
10.5752745726417));
#133821=CARTESIAN_POINT('Ctrl Pts',(-21.0682129788551,18.1597865253222,
10.5794902640381));
#133822=CARTESIAN_POINT('Ctrl Pts',(-21.1029682787106,18.2369604523702,
10.583700913703));
#133823=CARTESIAN_POINT('Ctrl Pts',(-21.1339334100817,18.3159509969196,
10.587911563368));
#133824=CARTESIAN_POINT('Ctrl Pts',(-21.1609223976387,18.3963542635971,
10.592122213033));
#133825=CARTESIAN_POINT('Ctrl Pts',(-21.1878844462894,18.4766772762055,
10.5963286598616));
#133826=CARTESIAN_POINT('Ctrl Pts',(-21.2108781024617,18.5584097818782,
10.6005351066903));
#133827=CARTESIAN_POINT('Ctrl Pts',(-21.2297657078559,18.6411284956323,
10.6047415535189));
#133828=CARTESIAN_POINT('Ctrl Pts',(-21.24864245849,18.7237996707081,10.6089455828907));
#133829=CARTESIAN_POINT('Ctrl Pts',(-21.2634177498248,18.8074554899473,
10.6131496122625));
#133830=CARTESIAN_POINT('Ctrl Pts',(-21.2740042132099,18.8916591211951,
10.6173536416343));
#133831=CARTESIAN_POINT('Ctrl Pts',(-21.2845883389273,18.975844158876,10.6215567426862));
#133832=CARTESIAN_POINT('Ctrl Pts',(-21.2909854180498,19.0605763228041,
10.6257598437382));
#133833=CARTESIAN_POINT('Ctrl Pts',(-21.2931596531403,19.1454113596826,
10.6299629447901));
#133834=CARTESIAN_POINT('Ctrl Pts',(-21.2937333596144,19.1677964320698,
10.6310719997839));
#133835=CARTESIAN_POINT('Ctrl Pts',(-21.2940133304248,19.1901886456573,
10.6321810547777));
#133836=CARTESIAN_POINT('Ctrl Pts',(-21.2939995125392,19.2125798097912,
10.6332901097715));
#133837=CARTESIAN_POINT('',(-21.2940196853139,19.2096989556262,10.5667098967305));
#133838=CARTESIAN_POINT('Ctrl Pts',(-17.174464231106,17.180864983421,10.283238218494));
#133839=CARTESIAN_POINT('Ctrl Pts',(-17.2410686585138,17.1296999199839,
10.2874225029441));
#133840=CARTESIAN_POINT('Ctrl Pts',(-17.3101048654705,17.0818841653268,
10.2916067873942));
#133841=CARTESIAN_POINT('Ctrl Pts',(-17.3811936333275,17.0376351124834,
10.2957910718443));
#133842=CARTESIAN_POINT('Ctrl Pts',(-17.4120536962257,17.0184263317561,
10.2976074949616));
#133843=CARTESIAN_POINT('Ctrl Pts',(-17.4433002587604,16.9998890947577,
10.2994239180789));
#133844=CARTESIAN_POINT('Ctrl Pts',(-17.4749010481802,16.9820383965787,
10.3012403411962));
#133845=CARTESIAN_POINT('Ctrl Pts',(-17.5477022303472,16.9409143628506,
10.3054249755892));
#133846=CARTESIAN_POINT('Ctrl Pts',(-17.6226557687809,16.9032842410815,
10.3096096099823));
#133847=CARTESIAN_POINT('Ctrl Pts',(-17.6993922596291,16.8693794450073,
10.3137942443753));
#133848=CARTESIAN_POINT('Ctrl Pts',(-17.7760195255805,16.8355229082136,
10.3179729224593));
#133849=CARTESIAN_POINT('Ctrl Pts',(-17.8544242858621,16.8053813489309,
10.3221516005432));
#133850=CARTESIAN_POINT('Ctrl Pts',(-17.9342113535405,16.779141015397,10.3263302786272));
#133851=CARTESIAN_POINT('Ctrl Pts',(-18.0154285470652,16.752430342743,10.3305838565126));
#133852=CARTESIAN_POINT('Ctrl Pts',(-18.0980776713417,16.7297623675601,
10.334837434398));
#133853=CARTESIAN_POINT('Ctrl Pts',(-18.181719189663,16.7112828346924,10.3390910122835));
#133854=CARTESIAN_POINT('Ctrl Pts',(-18.2637391539387,16.6931615636292,
10.3432621262614));
#133855=CARTESIAN_POINT('Ctrl Pts',(-18.3467129067616,16.6790678856914,
10.3474332402394));
#133856=CARTESIAN_POINT('Ctrl Pts',(-18.4302110680641,16.6690888519004,
10.3516043542173));
#133857=CARTESIAN_POINT('Ctrl Pts',(-18.5136812107523,16.6591131666705,
10.3557740685377));
#133858=CARTESIAN_POINT('Ctrl Pts',(-18.5976749560381,16.6532494380237,
10.3599437828581));
#133859=CARTESIAN_POINT('Ctrl Pts',(-18.6817553300752,16.6515331620698,
10.3641134971784));
#133860=CARTESIAN_POINT('Ctrl Pts',(-18.7658327121718,16.6498169471884,
10.3682830631225));
#133861=CARTESIAN_POINT('Ctrl Pts',(-18.8499962569362,16.652247900101,10.3724526290665));
#133862=CARTESIAN_POINT('Ctrl Pts',(-18.9338078728663,16.6588094087744,
10.3766221950106));
#133863=CARTESIAN_POINT('Ctrl Pts',(-19.0205662018197,16.6656016119982,
10.3809383577495));
#133864=CARTESIAN_POINT('Ctrl Pts',(-19.106946868035,16.6768201947949,10.3852545204884));
#133865=CARTESIAN_POINT('Ctrl Pts',(-19.1924704625205,16.6923883119869,
10.3895706832273));
#133866=CARTESIAN_POINT('Ctrl Pts',(-19.2752081349112,16.7074492993989,
10.393746247419));
#133867=CARTESIAN_POINT('Ctrl Pts',(-19.357143268331,16.7265806476473,10.3979218116107));
#133868=CARTESIAN_POINT('Ctrl Pts',(-19.437854716723,16.749661230601,10.4020973758024));
#133869=CARTESIAN_POINT('Ctrl Pts',(-19.5226427085001,16.7739075589308,
10.4064838378149));
#133870=CARTESIAN_POINT('Ctrl Pts',(-19.6060795975567,16.8025123689437,
10.4108702998274));
#133871=CARTESIAN_POINT('Ctrl Pts',(-19.6877001821495,16.8352778018952,
10.41525676184));
#133872=CARTESIAN_POINT('Ctrl Pts',(-19.7693207667423,16.8680432348467,
10.4196432238525));
#133873=CARTESIAN_POINT('Ctrl Pts',(-19.8491245522344,16.9049689780518,
10.4240296858651));
#133874=CARTESIAN_POINT('Ctrl Pts',(-19.9266775857362,16.945802397917,10.4284161478776));
#133875=CARTESIAN_POINT('Ctrl Pts',(-20.0006622892055,16.9847570116046,
10.4326007822707));
#133876=CARTESIAN_POINT('Ctrl Pts',(-20.0728741952653,17.0274126045708,
10.4367854166637));
#133877=CARTESIAN_POINT('Ctrl Pts',(-20.1429187702869,17.0735838265015,
10.4409700510568));
#133878=CARTESIAN_POINT('Ctrl Pts',(-20.2128636455258,17.1196893294125,
10.4451487291407));
#133879=CARTESIAN_POINT('Ctrl Pts',(-20.2806469365539,17.1693002706272,
10.4493274072247));
#133880=CARTESIAN_POINT('Ctrl Pts',(-20.3458981308861,17.2221851731129,
10.4535060853086));
#133881=CARTESIAN_POINT('Ctrl Pts',(-20.4123189059815,17.276017999468,10.457759663194));
#133882=CARTESIAN_POINT('Ctrl Pts',(-20.4761154892317,17.3332430884428,
10.4620132410795));
#133883=CARTESIAN_POINT('Ctrl Pts',(-20.5369274194045,17.3935697481445,
10.4662668189649));
#133884=CARTESIAN_POINT('Ctrl Pts',(-20.5965603916461,17.4527268578301,
10.4704379329429));
#133885=CARTESIAN_POINT('Ctrl Pts',(-20.6533230631002,17.5148660125131,
10.4746090469208));
#133886=CARTESIAN_POINT('Ctrl Pts',(-20.7069098223473,17.5796732905743,
10.4787801608988));
#133887=CARTESIAN_POINT('Ctrl Pts',(-20.7604786000398,17.6444588219275,
10.4829498752191));
#133888=CARTESIAN_POINT('Ctrl Pts',(-20.8108732891324,17.7119103443124,
10.4871195895395));
#133889=CARTESIAN_POINT('Ctrl Pts',(-20.857827517359,17.7816796452479,10.4912893038599));
#133890=CARTESIAN_POINT('Ctrl Pts',(-20.9047800747525,17.8514464634921,
10.4954588698039));
#133891=CARTESIAN_POINT('Ctrl Pts',(-20.9482921585527,17.9235305141741,
10.499628435748));
#133892=CARTESIAN_POINT('Ctrl Pts',(-20.9881406062296,17.9975544398916,
10.503798001692));
#133893=CARTESIAN_POINT('Ctrl Pts',(-21.0293900761685,18.074180955519,10.5081141644309));
#133894=CARTESIAN_POINT('Ctrl Pts',(-21.0667132396991,18.1528858318598,
10.5124303271698));
#133895=CARTESIAN_POINT('Ctrl Pts',(-21.0999152164604,18.2332243669833,
10.5167464899088));
#133896=CARTESIAN_POINT('Ctrl Pts',(-21.1320356423208,18.3109458827751,
10.5209220541004));
#133897=CARTESIAN_POINT('Ctrl Pts',(-21.1602991397429,18.3901957994174,
10.5250976182921));
#133898=CARTESIAN_POINT('Ctrl Pts',(-21.1845795982611,18.4705544364463,
10.5292731824838));
#133899=CARTESIAN_POINT('Ctrl Pts',(-21.2100864050179,18.5549717971972,
10.5336596444963));
#133900=CARTESIAN_POINT('Ctrl Pts',(-21.2311970921469,18.6406122578467,
10.5380461065089));
#133901=CARTESIAN_POINT('Ctrl Pts',(-21.2478262226602,18.7269775601629,
10.5424325685214));
#133902=CARTESIAN_POINT('Ctrl Pts',(-21.2644553531735,18.813342862479,10.5468190305339));
#133903=CARTESIAN_POINT('Ctrl Pts',(-21.2766029222518,18.9004324212998,
10.5512054925465));
#133904=CARTESIAN_POINT('Ctrl Pts',(-21.2842464642989,18.9877446051473,
10.555591954559));
#133905=CARTESIAN_POINT('Ctrl Pts',(-21.2907042434478,19.0615118189368,
10.5592979331155));
#133906=CARTESIAN_POINT('Ctrl Pts',(-21.293961988618,19.1355632322755,10.563003911672));
#133907=CARTESIAN_POINT('Ctrl Pts',(-21.2939996693303,19.2096988355573,
10.5667098902285));
#133908=CARTESIAN_POINT('Ctrl Pts',(-21.2974135715529,19.2097193143547,
10.5667109992077));
#133909=CARTESIAN_POINT('Ctrl Pts',(-21.292595768045,19.9846331911651,10.6053965865519));
#133910=CARTESIAN_POINT('Ctrl Pts',(-20.5048168766745,21.6171665132323,
10.6864741094567));
#133911=CARTESIAN_POINT('Ctrl Pts',(-17.7257693111366,22.0652534087646,
10.8099435679219));
#133912=CARTESIAN_POINT('Ctrl Pts',(-15.7882884293495,19.9081907815984,
10.9371193746033));
#133913=CARTESIAN_POINT('Ctrl Pts',(-16.3366272769448,17.9036399517467,
11.0282736305002));
#133914=CARTESIAN_POINT('Ctrl Pts',(-17.0711420957025,17.2560799239325,
11.0770359508366));
#133915=CARTESIAN_POINT('Ctrl Pts',(-17.1731949711369,17.1791828613964,
11.0834063356124));
#133916=CARTESIAN_POINT('Origin',(-18.734,19.211,-1.76670989022852));
#133917=CARTESIAN_POINT('',(-17.174464231106,17.180864983421,11.9498687293772));
#133918=CARTESIAN_POINT('',(-17.174464231106,17.180864983421,11.8833305103542));
#133919=CARTESIAN_POINT('',(-17.174464231106,17.180864983421,-1.76670989022852));
#133920=CARTESIAN_POINT('',(-21.2940197026037,19.2123010442705,11.4332901032639));
#133921=CARTESIAN_POINT('Ctrl Pts',(-21.2939996693303,19.212301164443,11.4332901097715));
#133922=CARTESIAN_POINT('Ctrl Pts',(-21.293961988618,19.2864367677247,11.436996088328));
#133923=CARTESIAN_POINT('Ctrl Pts',(-21.2907042434478,19.3604881810636,
11.4407020668845));
#133924=CARTESIAN_POINT('Ctrl Pts',(-21.2842464642989,19.4342553948533,
11.444408045441));
#133925=CARTESIAN_POINT('Ctrl Pts',(-21.2769546129518,19.5175502156942,
11.4485926798341));
#133926=CARTESIAN_POINT('Ctrl Pts',(-21.2655641024497,19.6006424250678,
11.4527773142271));
#133927=CARTESIAN_POINT('Ctrl Pts',(-21.250093180474,19.6830965019697,11.4569619486202));
#133928=CARTESIAN_POINT('Ctrl Pts',(-21.2346442794409,19.7654332156989,
11.4611406267041));
#133929=CARTESIAN_POINT('Ctrl Pts',(-21.2151265874821,19.8471331528555,
11.465319304788));
#133930=CARTESIAN_POINT('Ctrl Pts',(-21.1916101807318,19.9277650937117,
11.469497982872));
#133931=CARTESIAN_POINT('Ctrl Pts',(-21.1676722592913,20.0098423041587,
11.4737515607574));
#133932=CARTESIAN_POINT('Ctrl Pts',(-21.1395909011584,20.0908123737399,
11.4780051386429));
#133933=CARTESIAN_POINT('Ctrl Pts',(-21.107494673889,20.170230437914,11.4822587165283));
#133934=CARTESIAN_POINT('Ctrl Pts',(-21.0760206946157,20.2481088279425,
11.4864298305062));
#133935=CARTESIAN_POINT('Ctrl Pts',(-21.0406863094725,20.3244944066984,
11.4906009444842));
#133936=CARTESIAN_POINT('Ctrl Pts',(-21.0016627302193,20.3989838980282,
11.4947720584621));
#133937=CARTESIAN_POINT('Ctrl Pts',(-20.962652245705,20.4734483936899,11.4989417727825));
#133938=CARTESIAN_POINT('Ctrl Pts',(-20.9199552389621,20.5460176583684,
11.5031114871029));
#133939=CARTESIAN_POINT('Ctrl Pts',(-20.873789724926,20.6163113295996,11.5072812014233));
#133940=CARTESIAN_POINT('Ctrl Pts',(-20.827625853657,20.6866024994803,11.5114507673673));
#133941=CARTESIAN_POINT('Ctrl Pts',(-20.7779939737414,20.7546178528605,
11.5156203333114));
#133942=CARTESIAN_POINT('Ctrl Pts',(-20.7251556946207,20.8200055934581,
11.5197898992554));
#133943=CARTESIAN_POINT('Ctrl Pts',(-20.6704596867893,20.8876922863505,
11.5241060619943));
#133944=CARTESIAN_POINT('Ctrl Pts',(-20.6123279420986,20.9525627446113,
11.5284222247332));
#133945=CARTESIAN_POINT('Ctrl Pts',(-20.5510951122121,21.0142651921375,
11.5327383874721));
#133946=CARTESIAN_POINT('Ctrl Pts',(-20.4918569353186,21.0739576889255,
11.5369139516638));
#133947=CARTESIAN_POINT('Ctrl Pts',(-20.4297169860235,21.1306851185865,
11.5410895158555));
#133948=CARTESIAN_POINT('Ctrl Pts',(-20.3650134540522,21.1841687998498,
11.5452650800472));
#133949=CARTESIAN_POINT('Ctrl Pts',(-20.2970419004992,21.2403538147082,
11.5496515420597));
#133950=CARTESIAN_POINT('Ctrl Pts',(-20.2262414538862,21.2929584378006,
11.5540380040723));
#133951=CARTESIAN_POINT('Ctrl Pts',(-20.1530384991425,21.3417110873958,
11.5584244660848));
#133952=CARTESIAN_POINT('Ctrl Pts',(-20.0798355443987,21.390463736991,11.5628109280973));
#133953=CARTESIAN_POINT('Ctrl Pts',(-20.0042306192381,21.4353641822177,
11.5671973901099));
#133954=CARTESIAN_POINT('Ctrl Pts',(-19.9266775857363,21.4761976020829,
11.5715838521224));
#133955=CARTESIAN_POINT('Ctrl Pts',(-19.852692882267,21.5151522157705,11.5757684865155));
#133956=CARTESIAN_POINT('Ctrl Pts',(-19.7766600165144,21.5505508359911,
11.5799531209085));
#133957=CARTESIAN_POINT('Ctrl Pts',(-19.6989550698443,21.5821730668978,
11.5841377553015));
#133958=CARTESIAN_POINT('Ctrl Pts',(-19.6213607265478,21.6137502874729,
11.5883164333855));
#133959=CARTESIAN_POINT('Ctrl Pts',(-19.5420994522194,21.6415616236984,
11.5924951114694));
#133960=CARTESIAN_POINT('Ctrl Pts',(-19.4615717652905,21.6654325874532,
11.5966737895534));
#133961=CARTESIAN_POINT('Ctrl Pts',(-19.3796006774476,21.6897314210775,
11.6009273674388));
#133962=CARTESIAN_POINT('Ctrl Pts',(-19.2963177561688,21.7099470058045,
11.6051809453242));
#133963=CARTESIAN_POINT('Ctrl Pts',(-19.2121666533116,21.7259466498637,
11.6094345232097));
#133964=CARTESIAN_POINT('Ctrl Pts',(-19.1296469837907,21.7416361096021,
11.6136056371876));
#133965=CARTESIAN_POINT('Ctrl Pts',(-19.0462929678286,21.7532715484977,
11.6177767511656));
#133966=CARTESIAN_POINT('Ctrl Pts',(-18.9625363705287,21.760778642813,11.6219478651435));
#133967=CARTESIAN_POINT('Ctrl Pts',(-18.878807878564,21.7682832180503,11.6261175794639));
#133968=CARTESIAN_POINT('Ctrl Pts',(-18.7946775313674,21.7716621589129,
11.6302872937843));
#133969=CARTESIAN_POINT('Ctrl Pts',(-18.7105831609272,21.7708928984721,
11.6344570081046));
#133970=CARTESIAN_POINT('Ctrl Pts',(-18.6264917829255,21.7701236654048,
11.6386265740487));
#133971=CARTESIAN_POINT('Ctrl Pts',(-18.5424368391406,21.7652065295826,
11.6427961399927));
#133972=CARTESIAN_POINT('Ctrl Pts',(-18.4588557388015,21.75617104249,11.6469657059368));
#133973=CARTESIAN_POINT('Ctrl Pts',(-18.3723360300829,21.7468178788176,
11.6512818686757));
#133974=CARTESIAN_POINT('Ctrl Pts',(-18.2863246298127,21.7330514297719,
11.6555980314146));
#133975=CARTESIAN_POINT('Ctrl Pts',(-18.201298466622,21.7149626747092,11.6599141941535));
#133976=CARTESIAN_POINT('Ctrl Pts',(-18.1190420217542,21.6974631589401,
11.6640897583452));
#133977=CARTESIAN_POINT('Ctrl Pts',(-18.0377080547437,21.6759187771978,
11.6682653225369));
#133978=CARTESIAN_POINT('Ctrl Pts',(-17.9577139481209,21.6504630486355,
11.6724408867286));
#133979=CARTESIAN_POINT('Ctrl Pts',(-17.8736795293404,21.6237216117387,
11.6768273487411));
#133980=CARTESIAN_POINT('Ctrl Pts',(-17.7911244272666,21.592663525305,11.6812138107537));
#133981=CARTESIAN_POINT('Ctrl Pts',(-17.710507793232,21.5575003095429,11.6856002727662));
#133982=CARTESIAN_POINT('Ctrl Pts',(-17.6298911591974,21.5223370937809,
11.6899867347788));
#133983=CARTESIAN_POINT('Ctrl Pts',(-17.5512134783825,21.4830690758564,
11.6943731967913));
#133984=CARTESIAN_POINT('Ctrl Pts',(-17.4749010481796,21.4399616034209,
11.6987596588039));
#133985=CARTESIAN_POINT('Ctrl Pts',(-17.4020998660126,21.3988375696928,
11.7029442931969));
#133986=CARTESIAN_POINT('Ctrl Pts',(-17.3311800802056,21.3540665637942,
11.70712892759));
#133987=CARTESIAN_POINT('Ctrl Pts',(-17.262530574498,21.3058455145458,11.711313561983));
#133988=CARTESIAN_POINT('Ctrl Pts',(-17.1939787828646,21.2576931019925,
11.7154922400669));
#133989=CARTESIAN_POINT('Ctrl Pts',(-17.1276912258534,21.206100662466,11.7196709181509));
#133990=CARTESIAN_POINT('Ctrl Pts',(-17.0640314133914,21.1513105214734,
11.7238495962348));
#133991=CARTESIAN_POINT('Ctrl Pts',(-16.9992305445425,21.0955383065804,
11.7281031741203));
#133992=CARTESIAN_POINT('Ctrl Pts',(-16.9371529712701,21.0364528621869,
11.7323567520057));
#133993=CARTESIAN_POINT('Ctrl Pts',(-16.8781504066902,20.9743554057568,
11.7366103298911));
#133994=CARTESIAN_POINT('Ctrl Pts',(-16.8202917219587,20.9134618296928,
11.7407814438691));
#133995=CARTESIAN_POINT('Ctrl Pts',(-16.7653902112892,20.8496723357183,
11.744952557847));
#133996=CARTESIAN_POINT('Ctrl Pts',(-16.7137420754446,20.7833097399275,
11.749123671825));
#133997=CARTESIAN_POINT('Ctrl Pts',(-16.6621112706308,20.7169694127468,
11.7532933861454));
#133998=CARTESIAN_POINT('Ctrl Pts',(-16.613731954815,20.6480580612727,11.7574631004657));
#133999=CARTESIAN_POINT('Ctrl Pts',(-16.5688600933643,20.5769316178687,
11.7616328147861));
#134000=CARTESIAN_POINT('Ctrl Pts',(-16.5239898286469,20.5058077054487,
11.7658023807301));
#134001=CARTESIAN_POINT('Ctrl Pts',(-16.4826270148771,20.4324692473491,
11.7699719466742));
#134002=CARTESIAN_POINT('Ctrl Pts',(-16.4449835652526,20.3573000311682,
11.7741415126182));
#134003=CARTESIAN_POINT('Ctrl Pts',(-16.4060166183775,20.2794879580777,
11.7784576753571));
#134004=CARTESIAN_POINT('Ctrl Pts',(-16.3710356838063,20.1997144642827,
11.7827738380961));
#134005=CARTESIAN_POINT('Ctrl Pts',(-16.3402224147201,20.1184298166865,
11.787090000835));
#134006=CARTESIAN_POINT('Ctrl Pts',(-16.3104128846334,20.039793007936,11.7912655650267));
#134007=CARTESIAN_POINT('Ctrl Pts',(-16.2845037664843,19.9597424478439,
11.7954411292183));
#134008=CARTESIAN_POINT('Ctrl Pts',(-16.2626087130421,19.8787013604513,
11.79961669341));
#134009=CARTESIAN_POINT('Ctrl Pts',(-16.2396077925011,19.7935670803915,
11.8040031554226));
#134010=CARTESIAN_POINT('Ctrl Pts',(-16.2210372171719,19.7073401510525,
11.8083896174351));
#134011=CARTESIAN_POINT('Ctrl Pts',(-16.2069676619408,19.6205211379197,
11.8127760794476));
#134012=CARTESIAN_POINT('Ctrl Pts',(-16.1928981067097,19.5337021247869,
11.8171625414602));
#134013=CARTESIAN_POINT('Ctrl Pts',(-16.1833295591006,19.4462916129091,
11.8215490034727));
#134014=CARTESIAN_POINT('Ctrl Pts',(-16.1782696504243,19.3587916785811,
11.8259354654852));
#134015=CARTESIAN_POINT('Ctrl Pts',(-16.1734424727603,19.2753163125975,
11.8301201717331));
#134016=CARTESIAN_POINT('Ctrl Pts',(-16.1727003261448,19.191448852862,11.834304877981));
#134017=CARTESIAN_POINT('Ctrl Pts',(-16.1760881218677,19.1076229052962,
11.8384895842288));
#134018=CARTESIAN_POINT('Ctrl Pts',(-16.1794710795838,19.0239166669836,
11.8426683144266));
#134019=CARTESIAN_POINT('Ctrl Pts',(-16.1869722459979,18.9402522788471,
11.8468470446244));
#134020=CARTESIAN_POINT('Ctrl Pts',(-16.1985846232539,18.8570665777874,
11.8510257748222));
#134021=CARTESIAN_POINT('Ctrl Pts',(-16.2101833131975,18.7739789263039,
11.8551995796215));
#134022=CARTESIAN_POINT('Ctrl Pts',(-16.2258835179279,18.6913692935071,
11.8593733844208));
#134023=CARTESIAN_POINT('Ctrl Pts',(-16.2456263033231,18.6096711833892,
11.8635471892201));
#134024=CARTESIAN_POINT('Ctrl Pts',(-16.2653562958445,18.5280260117797,
11.8677182894893));
#134025=CARTESIAN_POINT('Ctrl Pts',(-16.2891235604505,18.4472916360286,
11.8718893897585));
#134026=CARTESIAN_POINT('Ctrl Pts',(-16.3168179573514,18.3678920752969,
11.8760604900277));
#134027=CARTESIAN_POINT('Ctrl Pts',(-16.3445027167179,18.2885201452806,
11.8802301387714));
#134028=CARTESIAN_POINT('Ctrl Pts',(-16.3761117424971,18.2104825415902,
11.8843997875151));
#134029=CARTESIAN_POINT('Ctrl Pts',(-16.4114852391776,18.1341874881103,
11.8885694362588));
#134030=CARTESIAN_POINT('Ctrl Pts',(-16.4468570371505,18.0578960984751,
11.8927388847675));
#134031=CARTESIAN_POINT('Ctrl Pts',(-16.4859927520556,17.983347509486,11.8969083332761));
#134032=CARTESIAN_POINT('Ctrl Pts',(-16.528685277592,17.9109280884772,11.9010777817847));
#134033=CARTESIAN_POINT('Ctrl Pts',(-16.5714158514221,17.8384441260677,
11.9052509461757));
#134034=CARTESIAN_POINT('Ctrl Pts',(-16.617709334547,17.768093519667,11.9094241105667));
#134035=CARTESIAN_POINT('Ctrl Pts',(-16.6673139151783,17.7002357474429,
11.9135972749577));
#134036=CARTESIAN_POINT('Ctrl Pts',(-16.7169399758737,17.6323485910517,
11.9177722464365));
#134037=CARTESIAN_POINT('Ctrl Pts',(-16.7698797016504,17.5669567780992,
11.9219472179154));
#134038=CARTESIAN_POINT('Ctrl Pts',(-16.8258408816674,17.5043867517436,
11.9261221893943));
#134039=CARTESIAN_POINT('Ctrl Pts',(-16.8818951704667,17.4417126207399,
11.9303041072334));
#134040=CARTESIAN_POINT('Ctrl Pts',(-16.9409806348315,17.3818699858574,
11.9344860250724));
#134041=CARTESIAN_POINT('Ctrl Pts',(-17.0027682222049,17.3251483272663,
11.9386679429114));
#134042=CARTESIAN_POINT('Ctrl Pts',(-17.0579318735125,17.2745075120295,
11.9424015384));
#134043=CARTESIAN_POINT('Ctrl Pts',(-17.1152486738755,17.2263539675634,
11.9461351338886));
#134044=CARTESIAN_POINT('Ctrl Pts',(-17.174464231106,17.180864983421,11.9498687293772));
#134045=CARTESIAN_POINT('Ctrl Pts',(-17.175718110251,17.1824653653533,11.1497835165008));
#134046=CARTESIAN_POINT('Ctrl Pts',(-17.3887251657916,17.01592042969,11.1632078216932));
#134047=CARTESIAN_POINT('Ctrl Pts',(-18.377772028057,16.4618739124435,11.2190240624461));
#134048=CARTESIAN_POINT('Ctrl Pts',(-20.5048168878155,16.8048334715693,
11.3135258905415));
#134049=CARTESIAN_POINT('Ctrl Pts',(-21.2925957841654,18.43736680388,11.3946034134446));
#134050=CARTESIAN_POINT('Ctrl Pts',(-21.297413587737,19.2122806855485,11.4332890007871));
#134051=CARTESIAN_POINT('',(-21.2939995125392,19.2094201902091,11.3667098902285));
#134052=CARTESIAN_POINT('Ctrl Pts',(-17.1731949711369,17.1791828613964,
11.0834063356124));
#134053=CARTESIAN_POINT('Ctrl Pts',(-17.7502563205703,16.7443658855329,
11.119427886397));
#134054=CARTESIAN_POINT('Ctrl Pts',(-19.4306371353495,16.3338524651331,
11.1978413727421));
#134055=CARTESIAN_POINT('Ctrl Pts',(-21.0857646400936,17.7107520667789,
11.2922755723032));
#134056=CARTESIAN_POINT('Ctrl Pts',(-21.2926072565653,18.8863578111491,
11.3506882210795));
#134057=CARTESIAN_POINT('Ctrl Pts',(-21.2907952889915,19.209402892007,11.3667089342955));
#134058=CARTESIAN_POINT('Ctrl Pts',(-21.2939995125392,19.2094201902091,
11.3667098902285));
#134059=CARTESIAN_POINT('Ctrl Pts',(-21.2940518853803,19.2942876523606,
11.3709134538372));
#134060=CARTESIAN_POINT('Ctrl Pts',(-21.2898797137862,19.3791700299233,
11.3751170174459));
#134061=CARTESIAN_POINT('Ctrl Pts',(-21.2815050782104,19.4636220031829,
11.3793205810546));
#134062=CARTESIAN_POINT('Ctrl Pts',(-21.2731292177987,19.5480863280015,
11.3835247594572));
#134063=CARTESIAN_POINT('Ctrl Pts',(-21.2605497166712,19.6321196761629,
11.3877289378599));
#134064=CARTESIAN_POINT('Ctrl Pts',(-21.2438404672875,19.7152824890537,
11.3919331162626));
#134065=CARTESIAN_POINT('Ctrl Pts',(-21.2271240709727,19.7984808725961,
11.3961390928892));
#134066=CARTESIAN_POINT('Ctrl Pts',(-21.2062745049673,19.880807540606,11.4003450695159));
#134067=CARTESIAN_POINT('Ctrl Pts',(-21.1814163656275,19.9618349574033,
11.4045510461425));
#134068=CARTESIAN_POINT('Ctrl Pts',(-21.1565238219895,20.0429745182095,
11.408762843948));
#134069=CARTESIAN_POINT('Ctrl Pts',(-21.1276117659035,20.1228108093803,
11.4129746417534));
#134070=CARTESIAN_POINT('Ctrl Pts',(-21.0948539828414,20.2009335693377,
11.4171864395589));
#134071=CARTESIAN_POINT('Ctrl Pts',(-21.0620694457195,20.2791201340097,
11.4214016772397));
#134072=CARTESIAN_POINT('Ctrl Pts',(-21.0254331231615,20.3555899771933,
11.4256169149205));
#134073=CARTESIAN_POINT('Ctrl Pts',(-20.9851650013542,20.4299569872141,
11.4298321526013));
#134074=CARTESIAN_POINT('Ctrl Pts',(-20.9448260993909,20.5044547137502,
11.4340547994973));
#134075=CARTESIAN_POINT('Ctrl Pts',(-20.9008428915854,20.5768418481601,
11.4382774463933));
#134076=CARTESIAN_POINT('Ctrl Pts',(-20.8534787082554,20.6467611240217,
11.4425000932893));
#134077=CARTESIAN_POINT('Ctrl Pts',(-20.8410561777284,20.6650993339886,
11.4436075959693));
#134078=CARTESIAN_POINT('Ctrl Pts',(-20.8284012848672,20.6832679625288,
11.4447150986492));
#134079=CARTESIAN_POINT('Ctrl Pts',(-20.8155192213964,20.7012609606902,
11.4458226013291));
#134080=CARTESIAN_POINT('Ctrl Pts',(-20.7668450946151,20.7692464566218,
11.4500072357222));
#134081=CARTESIAN_POINT('Ctrl Pts',(-20.7147461245074,20.8349713096213,
11.4541918701152));
#134082=CARTESIAN_POINT('Ctrl Pts',(-20.6594597008472,20.8980699275411,
11.4583765045082));
#134083=CARTESIAN_POINT('Ctrl Pts',(-20.6042519705679,20.9610787323882,
11.4625551825922));
#134084=CARTESIAN_POINT('Ctrl Pts',(-20.5458660991118,21.0214683841929,
11.4667338606761));
#134085=CARTESIAN_POINT('Ctrl Pts',(-20.4845818988862,21.0789033741851,
11.4709125387601));
#134086=CARTESIAN_POINT('Ctrl Pts',(-20.4221992234157,21.1373678450951,
11.4751661166455));
#134087=CARTESIAN_POINT('Ctrl Pts',(-20.356813572753,21.1927702956727,11.4794196945309));
#134088=CARTESIAN_POINT('Ctrl Pts',(-20.2887620518457,21.2447932446885,
11.4836732724164));
#134089=CARTESIAN_POINT('Ctrl Pts',(-20.2220298424627,21.2958076273232,
11.4878443863943));
#134090=CARTESIAN_POINT('Ctrl Pts',(-20.1527345889113,21.3435720832561,
11.4920155003723));
#134091=CARTESIAN_POINT('Ctrl Pts',(-20.0812289339452,21.3878266351597,
11.4961866143502));
#134092=CARTESIAN_POINT('Ctrl Pts',(-20.0097472733923,21.4320663370211,
11.5003563286706));
#134093=CARTESIAN_POINT('Ctrl Pts',(-19.9360570753465,21.4727982320514,
11.504526042991));
#134094=CARTESIAN_POINT('Ctrl Pts',(-19.860539605792,21.5098058892786,11.5086957573113));
#134095=CARTESIAN_POINT('Ctrl Pts',(-19.7850248234731,21.5468122296146,
11.5128653232554));
#134096=CARTESIAN_POINT('Ctrl Pts',(-19.7076833123974,21.5800943939657,
11.5170348891994));
#134097=CARTESIAN_POINT('Ctrl Pts',(-19.6289193227221,21.6094827299396,
11.5212044551435));
#134098=CARTESIAN_POINT('Ctrl Pts',(-19.5473860883357,21.639904323552,11.5255206178824));
#134099=CARTESIAN_POINT('Ctrl Pts',(-19.4643289796732,21.6661529958306,
11.5298367806213));
#134100=CARTESIAN_POINT('Ctrl Pts',(-19.3802151086566,21.6880962906887,
11.5341529433602));
#134101=CARTESIAN_POINT('Ctrl Pts',(-19.2988412381411,21.7093247850249,
11.5383285075519));
#134102=CARTESIAN_POINT('Ctrl Pts',(-19.2164788667996,21.7265240396988,
11.5425040717436));
#134103=CARTESIAN_POINT('Ctrl Pts',(-19.1335609462714,21.7396263168398,
11.5466796359353));
#134104=CARTESIAN_POINT('Ctrl Pts',(-19.0464550386958,21.7533903588514,
11.5510660979478));
#134105=CARTESIAN_POINT('Ctrl Pts',(-18.9587365661208,21.7626326086006,
11.5554525599603));
#134106=CARTESIAN_POINT('Ctrl Pts',(-18.8709107816374,21.7673363311332,
11.5598390219729));
#134107=CARTESIAN_POINT('Ctrl Pts',(-18.7830849971541,21.7720400536657,
11.5642254839854));
#134108=CARTESIAN_POINT('Ctrl Pts',(-18.6951524811213,21.7722053239559,
11.568611945998));
#134109=CARTESIAN_POINT('Ctrl Pts',(-18.6076132463771,21.7678782506229,
11.5729984080105));
#134110=CARTESIAN_POINT('Ctrl Pts',(-18.5241018215878,21.7637502723483,
11.5771830424035));
#134111=CARTESIAN_POINT('Ctrl Pts',(-18.4406374370146,21.7555188996868,
11.5813676767966));
#134112=CARTESIAN_POINT('Ctrl Pts',(-18.3576559923796,21.7431858517747,
11.5855523111896));
#134113=CARTESIAN_POINT('Ctrl Pts',(-18.2747926615599,21.7308703584299,
11.5897309892736));
#134114=CARTESIAN_POINT('Ctrl Pts',(-18.192411356418,21.7144648534413,11.5939096673575));
#134115=CARTESIAN_POINT('Ctrl Pts',(-18.1109456438834,21.6940230102285,
11.5980883454415));
#134116=CARTESIAN_POINT('Ctrl Pts',(-18.028019717,21.6732147616674,11.6023419233269));
#134117=CARTESIAN_POINT('Ctrl Pts',(-17.9460430111254,21.6482240726707,
11.6065955012123));
#134118=CARTESIAN_POINT('Ctrl Pts',(-17.8654649462453,21.6191625485833,
11.6108490790978));
#134119=CARTESIAN_POINT('Ctrl Pts',(-17.786449044388,21.5906644388492,11.6150201930757));
#134120=CARTESIAN_POINT('Ctrl Pts',(-17.7087784893785,21.5582520908959,
11.6191913070537));
#134121=CARTESIAN_POINT('Ctrl Pts',(-17.632862759841,21.5220813006762,11.6233624210316));
#134122=CARTESIAN_POINT('Ctrl Pts',(-17.5569725045598,21.4859226479144,
11.627532135352));
#134123=CARTESIAN_POINT('Ctrl Pts',(-17.4828363202444,21.4460082553229,
11.6317018496724));
#134124=CARTESIAN_POINT('Ctrl Pts',(-17.4108425631371,21.4025415572775,
11.6358715639928));
#134125=CARTESIAN_POINT('Ctrl Pts',(-17.3388513678768,21.3590764059638,
11.6400411299368));
#134126=CARTESIAN_POINT('Ctrl Pts',(-17.2690028416267,21.3120594390257,
11.6442106958808));
#134127=CARTESIAN_POINT('Ctrl Pts',(-17.2016584481436,21.2617387372491,
11.6483802618249));
#134128=CARTESIAN_POINT('Ctrl Pts',(-17.1319463088639,21.2096488216754,
11.6526964245638));
#134129=CARTESIAN_POINT('Ctrl Pts',(-17.0649180918037,21.1540188458217,
11.6570125873027));
#134130=CARTESIAN_POINT('Ctrl Pts',(-17.0009380103942,21.0951698809246,
11.6613287500416));
#134131=CARTESIAN_POINT('Ctrl Pts',(-16.9390420734071,21.0382379148692,
11.6655043142333));
#134132=CARTESIAN_POINT('Ctrl Pts',(-16.8799990325861,20.9782938250442,
11.669679878425));
#134133=CARTESIAN_POINT('Ctrl Pts',(-16.8241001932717,20.9156649900374,
11.6738554426167));
#134134=CARTESIAN_POINT('Ctrl Pts',(-16.7653780364704,20.8498729214603,
11.6782419046292));
#134135=CARTESIAN_POINT('Ctrl Pts',(-16.7101264215567,20.7811182222701,
11.6826283666418));
#134136=CARTESIAN_POINT('Ctrl Pts',(-16.658632903894,20.7098166720451,11.6870148286543));
#134137=CARTESIAN_POINT('Ctrl Pts',(-16.6071393862313,20.6385151218201,
11.6914012906668));
#134138=CARTESIAN_POINT('Ctrl Pts',(-16.5594042169154,20.5646672491325,
11.6957877526794));
#134139=CARTESIAN_POINT('Ctrl Pts',(-16.5156592733602,20.4887184433712,
11.7001742146919));
#134140=CARTESIAN_POINT('Ctrl Pts',(-16.4739270995035,20.4162641547462,
11.704358849085));
#134141=CARTESIAN_POINT('Ctrl Pts',(-16.4356706929266,20.341628329944,11.708543483478));
#134142=CARTESIAN_POINT('Ctrl Pts',(-16.4011245523601,20.2651784221843,
11.712728117871));
#134143=CARTESIAN_POINT('Ctrl Pts',(-16.3666275839488,20.1888373314056,
11.716906795955));
#134144=CARTESIAN_POINT('Ctrl Pts',(-16.3358305794285,20.1106877022102,
11.7210854740389));
#134145=CARTESIAN_POINT('Ctrl Pts',(-16.3089230895031,20.0311231481764,
11.7252641521229));
#134146=CARTESIAN_POINT('Ctrl Pts',(-16.2815333021588,19.9501324566934,
11.7295177300083));
#134147=CARTESIAN_POINT('Ctrl Pts',(-16.258174080664,19.8676760341798,11.7337713078937));
#134148=CARTESIAN_POINT('Ctrl Pts',(-16.2389948450999,19.7841921815778,
11.7380248857792));
#134149=CARTESIAN_POINT('Ctrl Pts',(-16.2201874364424,19.7023268263638,
11.7421959997571));
#134150=CARTESIAN_POINT('Ctrl Pts',(-16.2053994934178,19.6194739920343,
11.7463671137351));
#134151=CARTESIAN_POINT('Ctrl Pts',(-16.194721659298,19.5360623147054,11.750538227713));
#134152=CARTESIAN_POINT('Ctrl Pts',(-16.1840474082286,19.4526786269704,
11.7547079420334));
#134153=CARTESIAN_POINT('Ctrl Pts',(-16.1774805853424,19.3687369245934,
11.7588776563538));
#134154=CARTESIAN_POINT('Ctrl Pts',(-16.1750603443919,19.2846738688846,
11.7630473706742));
#134155=CARTESIAN_POINT('Ctrl Pts',(-16.172640189564,19.2006138044999,11.7672169366182));
#134156=CARTESIAN_POINT('Ctrl Pts',(-16.1743663356855,19.1164328552362,
11.7713865025623));
#134157=CARTESIAN_POINT('Ctrl Pts',(-16.1802258395509,19.0325692363341,
11.7755560685063));
#134158=CARTESIAN_POINT('Ctrl Pts',(-16.1862913563437,18.9457570760484,
11.7798722312452));
#134159=CARTESIAN_POINT('Ctrl Pts',(-16.1967862597981,18.8592855021224,
11.7841883939841));
#134160=CARTESIAN_POINT('Ctrl Pts',(-16.2116377216372,18.7736345501844,
11.7885045567231));
#134161=CARTESIAN_POINT('Ctrl Pts',(-16.226005398669,18.690773668997,11.7926801209147));
#134162=CARTESIAN_POINT('Ctrl Pts',(-16.2444500136974,18.6086812165377,
11.7968556851064));
#134163=CARTESIAN_POINT('Ctrl Pts',(-16.2668539711945,18.527779338318,11.8010312492981));
#134164=CARTESIAN_POINT('Ctrl Pts',(-16.2903894993245,18.4427912985553,
11.8054177113106));
#134165=CARTESIAN_POINT('Ctrl Pts',(-16.3182946694534,18.3591178195347,
11.8098041733232));
#134166=CARTESIAN_POINT('Ctrl Pts',(-16.3503755250187,18.2772257434102,
11.8141906353357));
#134167=CARTESIAN_POINT('Ctrl Pts',(-16.382456380584,18.1953336672856,11.8185770973483));
#134168=CARTESIAN_POINT('Ctrl Pts',(-16.4187126130535,18.1152234912951,
11.8229635593608));
#134169=CARTESIAN_POINT('Ctrl Pts',(-16.4588952312817,18.0373312684769,
11.8273500213734));
#134170=CARTESIAN_POINT('Ctrl Pts',(-16.497232190989,17.9630167728226,11.8315350054498));
#134171=CARTESIAN_POINT('Ctrl Pts',(-16.5392854659847,17.8904443146189,
11.8357199895262));
#134172=CARTESIAN_POINT('Ctrl Pts',(-16.5848729683162,17.8200100641321,
11.8399049736025));
#134173=CARTESIAN_POINT('Ctrl Pts',(-16.6303841734332,17.7496936954514,
11.8440829535087));
#134174=CARTESIAN_POINT('Ctrl Pts',(-16.679417597685,17.6815088023829,11.8482609334148));
#134175=CARTESIAN_POINT('Ctrl Pts',(-16.7317449889595,17.6158276360332,
11.852438913321));
#134176=CARTESIAN_POINT('Ctrl Pts',(-16.784021729639,17.5502100461409,11.8566128491278));
#134177=CARTESIAN_POINT('Ctrl Pts',(-16.8395858226251,17.4870917295056,
11.8607867849346));
#134178=CARTESIAN_POINT('Ctrl Pts',(-16.8981658619793,17.4268158677766,
11.8649607207414));
#134179=CARTESIAN_POINT('Ctrl Pts',(-16.9567039826102,17.366583138268,11.8691316697619));
#134180=CARTESIAN_POINT('Ctrl Pts',(-17.018253441943,17.3091891512907,11.8733026187824));
#134181=CARTESIAN_POINT('Ctrl Pts',(-17.0825036449284,17.2549427950121,
11.8774735678028));
#134182=CARTESIAN_POINT('Ctrl Pts',(-17.1125775158831,17.2295514679395,
11.8794258819866));
#134183=CARTESIAN_POINT('Ctrl Pts',(-17.1432425623528,17.2048492548057,
11.8813781961704));
#134184=CARTESIAN_POINT('Ctrl Pts',(-17.174464231106,17.180864983421,11.8833305103542));
#134185=CARTESIAN_POINT('Origin',(-18.734,19.211,-1.76670989022852));
#134186=CARTESIAN_POINT('',(-17.174464231106,17.180864983421,12.7499597594996));
#134187=CARTESIAN_POINT('',(-17.175049467869,17.1816082633957,12.6831923912068));
#134188=CARTESIAN_POINT('',(-17.174464231106,17.180864983421,-1.76670989022852));
#134189=CARTESIAN_POINT('',(-21.2939989766127,19.2087109517328,12.2332901098107));
#134190=CARTESIAN_POINT('Ctrl Pts',(-21.2939989766127,19.2087109517328,
12.2332901098107));
#134191=CARTESIAN_POINT('Ctrl Pts',(-21.2940747905548,19.2934988599292,
12.2375129674107));
#134192=CARTESIAN_POINT('Ctrl Pts',(-21.2899336304853,19.3784221563149,
12.2417358250107));
#134193=CARTESIAN_POINT('Ctrl Pts',(-21.2815646644668,19.4630203967141,
12.2459586826108));
#134194=CARTESIAN_POINT('Ctrl Pts',(-21.2734134565487,19.5454174151129,
12.2500716626647));
#134195=CARTESIAN_POINT('Ctrl Pts',(-21.2612518149666,19.6275055813485,
12.2541846427187));
#134196=CARTESIAN_POINT('Ctrl Pts',(-21.2451224198776,19.7088596111236,
12.2582976227727));
#134197=CARTESIAN_POINT('Ctrl Pts',(-21.2290007459442,19.7901746966529,
12.2624086339395));
#134198=CARTESIAN_POINT('Ctrl Pts',(-21.20891517906,19.8707558783839,12.2665196451063));
#134199=CARTESIAN_POINT('Ctrl Pts',(-21.18495989447,19.9501857653523,12.2706306562731));
#134200=CARTESIAN_POINT('Ctrl Pts',(-21.1610084101081,20.0296030516903,
12.2747410152757));
#134201=CARTESIAN_POINT('Ctrl Pts',(-21.1331885645307,20.1078689519367,
12.2788513742782));
#134202=CARTESIAN_POINT('Ctrl Pts',(-21.1016446063279,20.184580514455,12.2829617332808));
#134203=CARTESIAN_POINT('Ctrl Pts',(-21.0685960771618,20.2649510340633,
12.2872681465249));
#134204=CARTESIAN_POINT('Ctrl Pts',(-21.0314595036716,20.3436147061448,
12.2915745597691));
#134205=CARTESIAN_POINT('Ctrl Pts',(-20.9904568914614,20.4201328698601,
12.2958809730133));
#134206=CARTESIAN_POINT('Ctrl Pts',(-20.9512718262788,20.4932591677037,
12.2999964933322));
#134207=CARTESIAN_POINT('Ctrl Pts',(-20.9085564982548,20.5644257408166,
12.304112013651));
#134208=CARTESIAN_POINT('Ctrl Pts',(-20.8625501361321,20.6332778624348,
12.3082275339699));
#134209=CARTESIAN_POINT('Ctrl Pts',(-20.8165130556112,20.70217595654,12.3123458022172));
#134210=CARTESIAN_POINT('Ctrl Pts',(-20.7671808550876,20.768756147345,12.3164640704645));
#134211=CARTESIAN_POINT('Ctrl Pts',(-20.7148334041511,20.8326963417974,
12.3205823387118));
#134212=CARTESIAN_POINT('Ctrl Pts',(-20.662405465351,20.8967348487665,12.3247069390843));
#134213=CARTESIAN_POINT('Ctrl Pts',(-20.6069533520093,20.9581249187391,
12.3288315394568));
#134214=CARTESIAN_POINT('Ctrl Pts',(-20.5487934990216,21.0165815007661,
12.3329561398293));
#134215=CARTESIAN_POINT('Ctrl Pts',(-20.5408850965646,21.0245302515484,
12.3335169906232));
#134216=CARTESIAN_POINT('Ctrl Pts',(-20.5329266770598,21.0324248251517,
12.3340778414171));
#134217=CARTESIAN_POINT('Ctrl Pts',(-20.5249190804941,21.040264564551,12.334638692211));
#134218=CARTESIAN_POINT('Ctrl Pts',(-20.4651725946906,21.0987586301398,
12.338823326604));
#134219=CARTESIAN_POINT('Ctrl Pts',(-20.4024461555817,21.154431359773,12.3430079609971));
#134220=CARTESIAN_POINT('Ctrl Pts',(-20.3370370650428,21.2069639696395,
12.3471925953901));
#134221=CARTESIAN_POINT('Ctrl Pts',(-20.2717210762482,21.2594218058381,
12.3513712734741));
#134222=CARTESIAN_POINT('Ctrl Pts',(-20.2037303762194,21.3087481146436,
12.355549951558));
#134223=CARTESIAN_POINT('Ctrl Pts',(-20.1333988170805,21.35466110912,12.3597286296419));
#134224=CARTESIAN_POINT('Ctrl Pts',(-20.0618066152904,21.4013970610254,
12.3639822075274));
#134225=CARTESIAN_POINT('Ctrl Pts',(-19.9877891536758,21.4445957903898,
12.3682357854128));
#134226=CARTESIAN_POINT('Ctrl Pts',(-19.9117335730787,21.484003218397,12.3724893632982));
#134227=CARTESIAN_POINT('Ctrl Pts',(-19.8371524783218,21.522646656515,12.3766604772762));
#134228=CARTESIAN_POINT('Ctrl Pts',(-19.7606120124672,21.5576442636059,
12.3808315912541));
#134229=CARTESIAN_POINT('Ctrl Pts',(-19.6825046263017,21.5888012898231,
12.3850027052321));
#134230=CARTESIAN_POINT('Ctrl Pts',(-19.604423449824,21.6199478609992,12.3891724195525));
#134231=CARTESIAN_POINT('Ctrl Pts',(-19.5247768242091,21.647256240463,12.3933421338728));
#134232=CARTESIAN_POINT('Ctrl Pts',(-19.4439778217473,21.6705795357392,
12.3975118481932));
#134233=CARTESIAN_POINT('Ctrl Pts',(-19.3631816944607,21.6939020010724,
12.4016814141372));
#134234=CARTESIAN_POINT('Ctrl Pts',(-19.2812337140823,21.7132395374009,
12.4058509800813));
#134235=CARTESIAN_POINT('Ctrl Pts',(-19.1985614595127,21.7284953128726,
12.4100205460253));
#134236=CARTESIAN_POINT('Ctrl Pts',(-19.1129825504594,21.7442874625898,
12.4143367087642));
#134237=CARTESIAN_POINT('Ctrl Pts',(-19.0266280073019,21.7557053858608,
12.4186528715032));
#134238=CARTESIAN_POINT('Ctrl Pts',(-18.9399808515258,21.762699803818,12.4229690342421));
#134239=CARTESIAN_POINT('Ctrl Pts',(-18.8561562177354,21.7694663793458,
12.4271445984338));
#134240=CARTESIAN_POINT('Ctrl Pts',(-18.7720582145672,21.7720932477196,
12.4313201626254));
#134241=CARTESIAN_POINT('Ctrl Pts',(-18.6881249777991,21.7705889283903,
12.4354957268171));
#134242=CARTESIAN_POINT('Ctrl Pts',(-18.599952472774,21.7690086294678,12.4398821888297));
#134243=CARTESIAN_POINT('Ctrl Pts',(-18.5119623987479,21.7628688832023,
12.4442686508422));
#134244=CARTESIAN_POINT('Ctrl Pts',(-18.4246552312348,21.7522409988109,
12.4486551128548));
#134245=CARTESIAN_POINT('Ctrl Pts',(-18.3373480637217,21.7416131144196,
12.4530415748673));
#134246=CARTESIAN_POINT('Ctrl Pts',(-18.2507243612258,21.7264972665759,
12.4574280368799));
#134247=CARTESIAN_POINT('Ctrl Pts',(-18.1652685194105,21.7070257416514,
12.4618144988924));
#134248=CARTESIAN_POINT('Ctrl Pts',(-18.0837446275532,21.6884501304525,
12.4659991332855));
#134249=CARTESIAN_POINT('Ctrl Pts',(-18.0029800405435,21.6658417144697,
12.4701837676785));
#134250=CARTESIAN_POINT('Ctrl Pts',(-17.9234037289843,21.6392779259005,
12.4743684020716));
#134251=CARTESIAN_POINT('Ctrl Pts',(-17.8439406844549,21.6127519475962,
12.4785470801555));
#134252=CARTESIAN_POINT('Ctrl Pts',(-17.7656629884269,21.5822819240424,
12.4827257582395));
#134253=CARTESIAN_POINT('Ctrl Pts',(-17.6889882869427,21.5479960461184,
12.4869044363234));
#134254=CARTESIAN_POINT('Ctrl Pts',(-17.6109392465396,21.5130956184734,
12.4911580142088));
#134255=CARTESIAN_POINT('Ctrl Pts',(-17.5345517033715,21.474241299649,12.4954115920943));
#134256=CARTESIAN_POINT('Ctrl Pts',(-17.4602488495091,21.4316210857828,
12.4996651699797));
#134257=CARTESIAN_POINT('Ctrl Pts',(-17.3873865014589,21.3898271479288,
12.5038362839577));
#134258=CARTESIAN_POINT('Ctrl Pts',(-17.3165291499246,21.3444122698725,
12.5080073979356));
#134259=CARTESIAN_POINT('Ctrl Pts',(-17.2480529748745,21.2956010262208,
12.5121785119136));
#134260=CARTESIAN_POINT('Ctrl Pts',(-17.1795997776663,21.2468061616532,
12.5163482262339));
#134261=CARTESIAN_POINT('Ctrl Pts',(-17.1135265443543,21.1946174617221,
12.5205179405543));
#134262=CARTESIAN_POINT('Ctrl Pts',(-17.0501803764602,21.1393027447427,
12.5246876548747));
#134263=CARTESIAN_POINT('Ctrl Pts',(-16.9868364626946,21.0839899960983,
12.5288572208187));
#134264=CARTESIAN_POINT('Ctrl Pts',(-16.9262197673613,21.0255517547983,
12.5330267867628));
#134265=CARTESIAN_POINT('Ctrl Pts',(-16.8686431510732,20.9642951337872,
12.5371963527068));
#134266=CARTESIAN_POINT('Ctrl Pts',(-16.8090422119848,20.9008848055495,
12.5415125154458));
#134267=CARTESIAN_POINT('Ctrl Pts',(-16.7526994690718,20.8344546059654,
12.5458286781847));
#134268=CARTESIAN_POINT('Ctrl Pts',(-16.6999178084323,20.765384005948,12.5501448409236));
#134269=CARTESIAN_POINT('Ctrl Pts',(-16.6488555048364,20.6985633734612,
12.5543204051153));
#134270=CARTESIAN_POINT('Ctrl Pts',(-16.6011260701748,20.6292721356224,
12.558495969307));
#134271=CARTESIAN_POINT('Ctrl Pts',(-16.5569594955243,20.5578833067018,
12.5626715334986));
#134272=CARTESIAN_POINT('Ctrl Pts',(-16.5105621721842,20.4828887977433,
12.5670579955112));
#134273=CARTESIAN_POINT('Ctrl Pts',(-16.4680973689511,20.4055797420145,
12.5714444575237));
#134274=CARTESIAN_POINT('Ctrl Pts',(-16.4297760239617,20.3264155585477,
12.5758309195363));
#134275=CARTESIAN_POINT('Ctrl Pts',(-16.3914546789723,20.2472513750809,
12.5802173815488));
#134276=CARTESIAN_POINT('Ctrl Pts',(-16.3572769476616,20.166232628037,12.5846038435613));
#134277=CARTESIAN_POINT('Ctrl Pts',(-16.3273937923111,20.0838382216157,
12.5889903055739));
#134278=CARTESIAN_POINT('Ctrl Pts',(-16.2988856052357,20.0052349039716,
12.5931749399669));
#134279=CARTESIAN_POINT('Ctrl Pts',(-16.274179366091,19.9250871608005,12.59735957436));
#134280=CARTESIAN_POINT('Ctrl Pts',(-16.2534421603042,19.8437976010731,
12.601544208753));
#134281=CARTESIAN_POINT('Ctrl Pts',(-16.2327344713631,19.7626237469723,
12.605722886837));
#134282=CARTESIAN_POINT('Ctrl Pts',(-16.2159847069801,19.6803117464869,
12.6099015649209));
#134283=CARTESIAN_POINT('Ctrl Pts',(-16.2033111427938,19.5972821611362,
12.6140802430049));
#134284=CARTESIAN_POINT('Ctrl Pts',(-16.1904104140777,19.5127643301403,
12.6183338208903));
#134285=CARTESIAN_POINT('Ctrl Pts',(-16.1817336190672,19.4275033890774,
12.6225873987757));
#134286=CARTESIAN_POINT('Ctrl Pts',(-16.177351748603,19.3419569342512,12.6268409766612));
#134287=CARTESIAN_POINT('Ctrl Pts',(-16.1730548292483,19.2580689643819,
12.6310120906391));
#134288=CARTESIAN_POINT('Ctrl Pts',(-16.1728878141637,19.17390693303,12.6351832046171));
#134289=CARTESIAN_POINT('Ctrl Pts',(-16.1768654907269,19.0899087059923,
12.639354318595));
#134290=CARTESIAN_POINT('Ctrl Pts',(-16.1808418325422,19.0059386653711,
12.6435240329154));
#134291=CARTESIAN_POINT('Ctrl Pts',(-16.1889600821296,18.922132779036,12.6476937472358));
#134292=CARTESIAN_POINT('Ctrl Pts',(-16.2011829261395,18.8389278694113,
12.6518634615561));
#134293=CARTESIAN_POINT('Ctrl Pts',(-16.2134053352083,18.7557259205741,
12.6560330275002));
#134294=CARTESIAN_POINT('Ctrl Pts',(-16.229731980592,18.673125360952,12.6602025934442));
#134295=CARTESIAN_POINT('Ctrl Pts',(-16.250073974422,18.5915554912211,12.6643721593883));
#134296=CARTESIAN_POINT('Ctrl Pts',(-16.2711311676606,18.5071177254978,
12.6686883221272));
#134297=CARTESIAN_POINT('Ctrl Pts',(-16.2964911945897,18.4237849880537,
12.6730044848661));
#134298=CARTESIAN_POINT('Ctrl Pts',(-16.3259989267241,18.3420173585728,
12.677320647605));
#134299=CARTESIAN_POINT('Ctrl Pts',(-16.3545454475878,18.2629133010218,
12.6814962117967));
#134300=CARTESIAN_POINT('Ctrl Pts',(-16.3869733753121,18.1852743669884,
12.6856717759884));
#134301=CARTESIAN_POINT('Ctrl Pts',(-16.4230935537342,18.1094958481208,
12.6898473401801));
#134302=CARTESIAN_POINT('Ctrl Pts',(-16.4610380765009,18.0298899364114,
12.6942338021926));
#134303=CARTESIAN_POINT('Ctrl Pts',(-16.5030573653642,17.9523378315092,
12.6986202642051));
#134304=CARTESIAN_POINT('Ctrl Pts',(-16.5488792984353,17.8772655738142,
12.7030067262177));
#134305=CARTESIAN_POINT('Ctrl Pts',(-16.5947012315064,17.8021933161192,
12.7073931882302));
#134306=CARTESIAN_POINT('Ctrl Pts',(-16.6443254185491,17.7296013416972,
12.7117796502428));
#134307=CARTESIAN_POINT('Ctrl Pts',(-16.6974308899397,17.6598758076968,
12.7161661122553));
#134308=CARTESIAN_POINT('Ctrl Pts',(-16.7480908287733,17.5933611681483,
12.7203505755777));
#134309=CARTESIAN_POINT('Ctrl Pts',(-16.8021070326387,17.5292072036809,
12.7245350389001));
#134310=CARTESIAN_POINT('Ctrl Pts',(-16.8592314426079,17.4677722879056,
12.7287195022225));
#134311=CARTESIAN_POINT('Ctrl Pts',(-16.916267765385,17.4064321062243,12.7328975130034));
#134312=CARTESIAN_POINT('Ctrl Pts',(-16.9764024587933,17.3478029746755,
12.7370755237843));
#134313=CARTESIAN_POINT('Ctrl Pts',(-17.0393460611034,17.2922118336351,
12.7412535345652));
#134314=CARTESIAN_POINT('Ctrl Pts',(-17.083067119491,17.2535978453334,12.7441556095433));
#134315=CARTESIAN_POINT('Ctrl Pts',(-17.1281425218688,17.2164490021399,
12.7470576845215));
#134316=CARTESIAN_POINT('Ctrl Pts',(-17.174464231106,17.180864983421,12.7499597594996));
#134317=CARTESIAN_POINT('Ctrl Pts',(-17.174464231106,17.180864983421,11.9498687293772));
#134318=CARTESIAN_POINT('Ctrl Pts',(-17.1916066861211,17.1676962672793,
11.9509495769737));
#134319=CARTESIAN_POINT('Ctrl Pts',(-17.2089081586167,17.1547506759101,
11.9520304245702));
#134320=CARTESIAN_POINT('Ctrl Pts',(-17.2263622218886,17.142032061628,11.9531112721667));
#134321=CARTESIAN_POINT('Ctrl Pts',(-17.2939377743557,17.0927903822928,
11.9572959065597));
#134322=CARTESIAN_POINT('Ctrl Pts',(-17.3640540780912,17.0467712239068,
11.9614805409528));
#134323=CARTESIAN_POINT('Ctrl Pts',(-17.436370866589,17.0042470387189,11.9656651753458));
#134324=CARTESIAN_POINT('Ctrl Pts',(-17.5085847210894,16.9617833814452,
11.9698438534298));
#134325=CARTESIAN_POINT('Ctrl Pts',(-17.5829924458182,16.9228050473159,
11.9740225315137));
#134326=CARTESIAN_POINT('Ctrl Pts',(-17.6592229568398,16.8875425961521,
11.9782012095977));
#134327=CARTESIAN_POINT('Ctrl Pts',(-17.7368198449856,16.8516480908938,
11.9824547874831));
#134328=CARTESIAN_POINT('Ctrl Pts',(-17.8163051194015,16.8196042772378,
11.9867083653685));
#134329=CARTESIAN_POINT('Ctrl Pts',(-17.8972589731899,16.7916065937817,
11.990961943254));
#134330=CARTESIAN_POINT('Ctrl Pts',(-17.9766433785542,16.7641517000523,
11.9951330572319));
#134331=CARTESIAN_POINT('Ctrl Pts',(-18.0574394740945,16.7405876095593,
11.9993041712099));
#134332=CARTESIAN_POINT('Ctrl Pts',(-18.1392307762334,16.721050287564,12.0034752851878));
#134333=CARTESIAN_POINT('Ctrl Pts',(-18.220994632511,16.7015195215058,12.0076449995082));
#134334=CARTESIAN_POINT('Ctrl Pts',(-18.3037525850822,16.6860129471901,
12.0118147138286));
#134335=CARTESIAN_POINT('Ctrl Pts',(-18.387074664491,16.6746161939521,12.015984428149));
#134336=CARTESIAN_POINT('Ctrl Pts',(-18.4703937789427,16.6632198462596,
12.020153994093));
#134337=CARTESIAN_POINT('Ctrl Pts',(-18.5542765244151,16.6559330903703,
12.024323560037));
#134338=CARTESIAN_POINT('Ctrl Pts',(-18.6382858147576,16.6527899236491,
12.0284931259811));
#134339=CARTESIAN_POINT('Ctrl Pts',(-18.7252487681119,16.6495362470634,
12.03280928872));
#134340=CARTESIAN_POINT('Ctrl Pts',(-18.8123468034839,16.6507229779045,
12.0371254514589));
#134341=CARTESIAN_POINT('Ctrl Pts',(-18.8990948495912,16.6563290445464,
12.0414416141978));
#134342=CARTESIAN_POINT('Ctrl Pts',(-18.9830170872209,16.6617524941571,
12.0456171783895));
#134343=CARTESIAN_POINT('Ctrl Pts',(-19.0666113245962,16.6713116809417,
12.0497927425812));
#134344=CARTESIAN_POINT('Ctrl Pts',(-19.1494452607508,16.6849348315375,
12.0539683067729));
#134345=CARTESIAN_POINT('Ctrl Pts',(-19.2364629421015,16.6992460550839,
12.0583547687854));
#134346=CARTESIAN_POINT('Ctrl Pts',(-19.3226409276425,16.7180424488712,
12.062741230798));
#134347=CARTESIAN_POINT('Ctrl Pts',(-19.4074943094425,16.7411810966898,
12.0671276928105));
#134348=CARTESIAN_POINT('Ctrl Pts',(-19.4923476912424,16.7643197445083,
12.071514154823));
#134349=CARTESIAN_POINT('Ctrl Pts',(-19.5758759419184,16.7918003927741,
12.0759006168356));
#134350=CARTESIAN_POINT('Ctrl Pts',(-19.6576188802165,16.8234221134992,
12.0802870788481));
#134351=CARTESIAN_POINT('Ctrl Pts',(-19.7356007047514,16.8535888719792,
12.0844717132412));
#134352=CARTESIAN_POINT('Ctrl Pts',(-19.8122481596155,16.8876362896631,
12.0886563476342));
#134353=CARTESIAN_POINT('Ctrl Pts',(-19.8871479757777,16.9254257295026,
12.0928409820273));
#134354=CARTESIAN_POINT('Ctrl Pts',(-19.9619411813225,16.9631613807519,
12.0970196601112));
#134355=CARTESIAN_POINT('Ctrl Pts',(-20.0349912820117,17.0046282689895,
12.1011983381951));
#134356=CARTESIAN_POINT('Ctrl Pts',(-20.1059035528266,17.0496391690091,
12.1053770162791));
#134357=CARTESIAN_POINT('Ctrl Pts',(-20.1780868751321,17.0954568570628,
12.1096305941645));
#134358=CARTESIAN_POINT('Ctrl Pts',(-20.2480545228571,17.1449466854561,
12.11388417205));
#134359=CARTESIAN_POINT('Ctrl Pts',(-20.3154149295587,17.1978614502303,
12.1181377499354));
#134360=CARTESIAN_POINT('Ctrl Pts',(-20.3814694233333,17.2497503590347,
12.1223088639133));
#134361=CARTESIAN_POINT('Ctrl Pts',(-20.4450164884365,17.3049322938692,
12.1264799778913));
#134362=CARTESIAN_POINT('Ctrl Pts',(-20.5057163649394,17.3631306533724,
12.1306510918693));
#134363=CARTESIAN_POINT('Ctrl Pts',(-20.5663958730124,17.4213094838539,
12.1348208061896));
#134364=CARTESIAN_POINT('Ctrl Pts',(-20.6242297581414,17.4825024106647,
12.13899052051));
#134365=CARTESIAN_POINT('Ctrl Pts',(-20.678913285295,17.5463942470714,12.1431602348304));
#134366=CARTESIAN_POINT('Ctrl Pts',(-20.733594866574,17.6102838099324,12.1473298007744));
#134367=CARTESIAN_POINT('Ctrl Pts',(-20.7851260142849,17.6768717413838,
12.1514993667185));
#134368=CARTESIAN_POINT('Ctrl Pts',(-20.8332415555807,17.7458089232721,
12.1556689326625));
#134369=CARTESIAN_POINT('Ctrl Pts',(-20.8830487799516,17.8171698514324,
12.1599850954014));
#134370=CARTESIAN_POINT('Ctrl Pts',(-20.9291954417205,17.8910478705134,
12.1643012581404));
#134371=CARTESIAN_POINT('Ctrl Pts',(-20.971436698905,17.9670237066595,12.1686174208793));
#134372=CARTESIAN_POINT('Ctrl Pts',(-21.0123019515797,18.0405246379345,
12.172792985071));
#134373=CARTESIAN_POINT('Ctrl Pts',(-21.0495121634691,18.1159883689943,
12.1769685492626));
#134374=CARTESIAN_POINT('Ctrl Pts',(-21.082893688299,18.1930125535797,12.1811441134543));
#134375=CARTESIAN_POINT('Ctrl Pts',(-21.117961234591,18.2739270466209,12.1855305754669));
#134376=CARTESIAN_POINT('Ctrl Pts',(-21.1488029510882,18.3565632259543,
12.1899170374794));
#134377=CARTESIAN_POINT('Ctrl Pts',(-21.1752765362398,18.4404360029143,
12.1943034994919));
#134378=CARTESIAN_POINT('Ctrl Pts',(-21.2017501213915,18.5243087798743,
12.1986899615045));
#134379=CARTESIAN_POINT('Ctrl Pts',(-21.2238555029592,18.6094175737551,
12.203076423517));
#134380=CARTESIAN_POINT('Ctrl Pts',(-21.2415125421985,18.6952666864385,
12.2074628855296));
#134381=CARTESIAN_POINT('Ctrl Pts',(-21.2654843862328,18.8118185902907,
12.2134181072291));
#134382=CARTESIAN_POINT('Ctrl Pts',(-21.2813366135111,18.9300931627089,
12.2193733289286));
#134383=CARTESIAN_POINT('Ctrl Pts',(-21.2888788651003,19.0491544419404,
12.2253285506281));
#134384=CARTESIAN_POINT('Ctrl Pts',(-21.2922399536336,19.1022122716411,
12.2279824036759));
#134385=CARTESIAN_POINT('Ctrl Pts',(-21.2939513313562,19.1554260264004,
12.2306362567237));
#134386=CARTESIAN_POINT('Ctrl Pts',(-21.293998976612,19.2087109509454,12.2332901097715));
#134387=CARTESIAN_POINT('',(-21.2939992159918,19.2130035272629,12.1667098902285));
#134388=CARTESIAN_POINT('Ctrl Pts',(-17.174464231106,17.180864983421,11.8833305103542));
#134389=CARTESIAN_POINT('Ctrl Pts',(-17.2411433188361,17.1296425664374,
11.8875000033358));
#134390=CARTESIAN_POINT('Ctrl Pts',(-17.3103631224993,17.0816975368105,
11.8916694963173));
#134391=CARTESIAN_POINT('Ctrl Pts',(-17.3817637625324,17.037280340504,11.8958389892988));
#134392=CARTESIAN_POINT('Ctrl Pts',(-17.4531714778517,16.9928587427751,
11.9000088954469));
#134393=CARTESIAN_POINT('Ctrl Pts',(-17.5267600673345,16.9519659143865,
11.904178801595));
#134394=CARTESIAN_POINT('Ctrl Pts',(-17.6021425997059,16.9148077551304,
11.9083487077431));
#134395=CARTESIAN_POINT('Ctrl Pts',(-17.677605069376,16.8776101925433,11.9125230357516));
#134396=CARTESIAN_POINT('Ctrl Pts',(-17.7548648666536,16.8441554099555,
11.91669736376));
#134397=CARTESIAN_POINT('Ctrl Pts',(-17.8335129580331,16.8146020599137,
11.9208716917685));
#134398=CARTESIAN_POINT('Ctrl Pts',(-17.9122052197822,16.7850321121088,
11.9250483641646));
#134399=CARTESIAN_POINT('Ctrl Pts',(-17.992286889851,16.7593680998778,11.9292250365607));
#134400=CARTESIAN_POINT('Ctrl Pts',(-18.073333887536,16.737718720436,11.9334017089567));
#134401=CARTESIAN_POINT('Ctrl Pts',(-18.1545199182313,16.7160322023157,
11.9375855462738));
#134402=CARTESIAN_POINT('Ctrl Pts',(-18.2366741336785,16.6983741672315,
11.9417693835909));
#134403=CARTESIAN_POINT('Ctrl Pts',(-18.3193626550843,16.6848020916403,
11.945953220908));
#134404=CARTESIAN_POINT('Ctrl Pts',(-18.3758384177107,16.6755324456675,
11.9488107566236));
#134405=CARTESIAN_POINT('Ctrl Pts',(-18.4325632674714,16.6681677378075,
11.9516682923392));
#134406=CARTESIAN_POINT('Ctrl Pts',(-18.4893986055749,16.662712308658,11.9545258280548));
#134407=CARTESIAN_POINT('Ctrl Pts',(-18.5726294499944,16.6547232653983,
11.9587104624479));
#134408=CARTESIAN_POINT('Ctrl Pts',(-18.6564069960725,16.6508013065455,
11.9628950968409));
#134409=CARTESIAN_POINT('Ctrl Pts',(-18.740299675164,16.6510077511655,11.967079731234));
#134410=CARTESIAN_POINT('Ctrl Pts',(-18.8240729434104,16.6512139019371,
11.9712584093179));
#134411=CARTESIAN_POINT('Ctrl Pts',(-18.907960563061,16.655536782935,11.9754370874018));
#134412=CARTESIAN_POINT('Ctrl Pts',(-18.9915257624718,16.6639859675174,
11.9796157654858));
#134413=CARTESIAN_POINT('Ctrl Pts',(-19.076588808025,16.6725865976611,11.9838693433712));
#134414=CARTESIAN_POINT('Ctrl Pts',(-19.1613172809479,16.6854629604527,
11.9881229212567));
#134415=CARTESIAN_POINT('Ctrl Pts',(-19.2452503475945,16.702569597919,11.9923764991421));
#134416=CARTESIAN_POINT('Ctrl Pts',(-19.3275562079622,16.7193445898371,
11.99654761312));
#134417=CARTESIAN_POINT('Ctrl Pts',(-19.4090967563144,16.7401871997923,
12.000718727098));
#134418=CARTESIAN_POINT('Ctrl Pts',(-19.4894442918863,16.7650024689595,
12.004889841076));
#134419=CARTESIAN_POINT('Ctrl Pts',(-19.5697648660668,16.7898094111234,
12.0090595553963));
#134420=CARTESIAN_POINT('Ctrl Pts',(-19.6488927833418,16.818586229372,12.0132292697167));
#134421=CARTESIAN_POINT('Ctrl Pts',(-19.7264143560957,16.8511877731872,
12.0173989840371));
#134422=CARTESIAN_POINT('Ctrl Pts',(-19.8039331702994,16.8837881568996,
12.0215685499811));
#134423=CARTESIAN_POINT('Ctrl Pts',(-19.8798453299034,16.9202128164538,
12.0257381159252));
#134424=CARTESIAN_POINT('Ctrl Pts',(-19.9537573024931,16.9602685360055,
12.0299076818692));
#134425=CARTESIAN_POINT('Ctrl Pts',(-20.0302679288587,17.0017325652425,
12.0342238446081));
#134426=CARTESIAN_POINT('Ctrl Pts',(-20.104634634367,17.0470874900865,12.0385400073471));
#134427=CARTESIAN_POINT('Ctrl Pts',(-20.1764506132334,17.0960682686236,
12.042856170086));
#134428=CARTESIAN_POINT('Ctrl Pts',(-20.2459271941418,17.1434535034518,
12.0470317342777));
#134429=CARTESIAN_POINT('Ctrl Pts',(-20.3130163291629,17.1942316733328,
12.0512072984693));
#134430=CARTESIAN_POINT('Ctrl Pts',(-20.3773824427361,17.2481209545907,
12.055382862661));
#134431=CARTESIAN_POINT('Ctrl Pts',(-20.44499953569,17.3047320553354,12.0597693246736));
#134432=CARTESIAN_POINT('Ctrl Pts',(-20.5096108706379,17.3647764140012,
12.0641557866861));
#134433=CARTESIAN_POINT('Ctrl Pts',(-20.5708718020377,17.4278841925218,
12.0685422486987));
#134434=CARTESIAN_POINT('Ctrl Pts',(-20.6321327334376,17.4909919710424,
12.0729287107112));
#134435=CARTESIAN_POINT('Ctrl Pts',(-20.6900429364134,17.5571626827011,
12.0773151727237));
#134436=CARTESIAN_POINT('Ctrl Pts',(-20.7443085775788,17.625989141074,12.0817016347363));
#134437=CARTESIAN_POINT('Ctrl Pts',(-20.796026764239,17.6915845997261,12.0858821780095));
#134438=CARTESIAN_POINT('Ctrl Pts',(-20.8446312405901,17.7598411080022,
12.0900627212828));
#134439=CARTESIAN_POINT('Ctrl Pts',(-20.8898359348525,17.8304307616065,
12.0942432645561));
#134440=CARTESIAN_POINT('Ctrl Pts',(-20.934977871844,17.9009224162288,12.0984180040186));
#134441=CARTESIAN_POINT('Ctrl Pts',(-20.9767291512529,17.9737404018926,
12.1025927434812));
#134442=CARTESIAN_POINT('Ctrl Pts',(-21.0148441174676,18.0485241457073,
12.1067674829438));
#134443=CARTESIAN_POINT('Ctrl Pts',(-21.0529176328928,18.1232265607022,
12.1109376822936));
#134444=CARTESIAN_POINT('Ctrl Pts',(-21.087362480976,18.199890080528,12.1151078816434));
#134445=CARTESIAN_POINT('Ctrl Pts',(-21.1179772351417,18.2781267276172,
12.1192780809931));
#134446=CARTESIAN_POINT('Ctrl Pts',(-21.1485693987601,18.3563056440885,
12.1234452031637));
#134447=CARTESIAN_POINT('Ctrl Pts',(-21.1753369141585,18.436054955007,12.1276123253342));
#134448=CARTESIAN_POINT('Ctrl Pts',(-21.198125670353,18.5169649283305,12.1317794475048));
#134449=CARTESIAN_POINT('Ctrl Pts',(-21.2209040463211,18.5978380473459,
12.1359446715607));
#134450=CARTESIAN_POINT('Ctrl Pts',(-21.2397071410263,18.6798703351908,
12.1401098956166));
#134451=CARTESIAN_POINT('Ctrl Pts',(-21.2544305326007,18.7626363860277,
12.1442751196726));
#134452=CARTESIAN_POINT('Ctrl Pts',(-21.2691564647158,18.8454167182569,
12.1484410624434));
#134453=CARTESIAN_POINT('Ctrl Pts',(-21.279801198365,18.9289306143289,12.1526070052143));
#134454=CARTESIAN_POINT('Ctrl Pts',(-21.2863115236392,19.0127428783158,
12.1567729479852));
#134455=CARTESIAN_POINT('Ctrl Pts',(-21.2914878410454,19.0793814658917,
12.1600852620663));
#134456=CARTESIAN_POINT('Ctrl Pts',(-21.2940514917317,19.1462084026767,
12.1633975761474));
#134457=CARTESIAN_POINT('Ctrl Pts',(-21.2939992159918,19.2130035272629,
12.1667098902285));
#134458=CARTESIAN_POINT('Ctrl Pts',(-21.2916489709697,19.2130199896839,
12.1667107986323));
#134459=CARTESIAN_POINT('Ctrl Pts',(-21.2937097175741,19.4962014444643,
12.1807663462274));
#134460=CARTESIAN_POINT('Ctrl Pts',(-21.1196060444512,20.6310006101477,
12.2372138293831));
#134461=CARTESIAN_POINT('Ctrl Pts',(-19.4558314911034,22.1507705593909,
12.3360532480991));
#134462=CARTESIAN_POINT('Ctrl Pts',(-16.6528318838468,21.4091880983477,
12.4632290547806));
#134463=CARTESIAN_POINT('Ctrl Pts',(-15.8397229951737,18.8995173453507,
12.5789421024831));
#134464=CARTESIAN_POINT('Ctrl Pts',(-16.6852502181462,17.565474461991,12.6522632146252));
#134465=CARTESIAN_POINT('Ctrl Pts',(-17.1750494678687,17.181608263396,12.6831923912067));
#134466=CARTESIAN_POINT('Origin',(-18.734,19.211,-1.76670989022852));
#134467=CARTESIAN_POINT('',(-17.174464231106,17.180864983421,13.5498657030158));
#134468=CARTESIAN_POINT('',(-17.174464231106,17.180864983421,13.4833228554268));
#134469=CARTESIAN_POINT('',(-17.174464231106,17.180864983421,-1.76670989022852));
#134470=CARTESIAN_POINT('',(-21.293999998394,19.2109093211998,13.0332901097364));
#134471=CARTESIAN_POINT('Ctrl Pts',(-21.293999998394,19.2109093219103,13.0332901097715));
#134472=CARTESIAN_POINT('Ctrl Pts',(-21.2940031178915,19.2989781543512,
13.0376462156856));
#134473=CARTESIAN_POINT('Ctrl Pts',(-21.2894573285641,19.3869643923453,
13.0420023215996));
#134474=CARTESIAN_POINT('Ctrl Pts',(-21.2804139262415,19.4743934627951,
13.0463584275137));
#134475=CARTESIAN_POINT('Ctrl Pts',(-21.2713470661107,19.5620493167382,
13.0507258327921));
#134476=CARTESIAN_POINT('Ctrl Pts',(-21.2577593163574,19.6491447181139,
13.0550932380704));
#134477=CARTESIAN_POINT('Ctrl Pts',(-21.2397536148681,19.7352125728896,
13.0594606433488));
#134478=CARTESIAN_POINT('Ctrl Pts',(-21.2217244341811,19.8213926590148,
13.0638337436661));
#134479=CARTESIAN_POINT('Ctrl Pts',(-21.1992659159006,19.9065421429604,
13.0682068439834));
#134480=CARTESIAN_POINT('Ctrl Pts',(-21.1725309633218,19.9902090482796,
13.0725799443008));
#134481=CARTESIAN_POINT('Ctrl Pts',(-21.1457232584227,20.0741036316349,
13.0769649448896));
#134482=CARTESIAN_POINT('Ctrl Pts',(-21.1146159900528,20.1565071961892,
13.0813499454785));
#134483=CARTESIAN_POINT('Ctrl Pts',(-21.0794107185111,20.2369866283209,
13.0857349460674));
#134484=CARTESIAN_POINT('Ctrl Pts',(-21.0474072811092,20.3101466511123,
13.0897211414781));
#134485=CARTESIAN_POINT('Ctrl Pts',(-21.0120180507083,20.3817167133685,
13.0937073368888));
#134486=CARTESIAN_POINT('Ctrl Pts',(-20.9734262024017,20.4513911818442,
13.0976935322996));
#134487=CARTESIAN_POINT('Ctrl Pts',(-20.9329131921061,20.524534153289,13.1018781666926));
#134488=CARTESIAN_POINT('Ctrl Pts',(-20.8887375841055,20.5958263313021,
13.1060628010856));
#134489=CARTESIAN_POINT('Ctrl Pts',(-20.8410930441,20.6648771968448,13.1102474354787));
#134490=CARTESIAN_POINT('Ctrl Pts',(-20.7935163202,20.7338297770271,13.1144261135626));
#134491=CARTESIAN_POINT('Ctrl Pts',(-20.742480730941,20.8005470061346,13.1186047916466));
#134492=CARTESIAN_POINT('Ctrl Pts',(-20.6882255495788,20.8646633579339,
13.1227834697305));
#134493=CARTESIAN_POINT('Ctrl Pts',(-20.6329978830832,20.9299289492597,
13.1270370476159));
#134494=CARTESIAN_POINT('Ctrl Pts',(-20.5744343004284,20.9924990829436,
13.1312906255014));
#134495=CARTESIAN_POINT('Ctrl Pts',(-20.5128330635404,21.0520195360331,
13.1355442033868));
#134496=CARTESIAN_POINT('Ctrl Pts',(-20.4524260868345,21.1103860689948,
13.1397153173648));
#134497=CARTESIAN_POINT('Ctrl Pts',(-20.3890985326093,21.1658197797779,
13.1438864313427));
#134498=CARTESIAN_POINT('Ctrl Pts',(-20.3231707254824,21.2180217749864,
13.1480575453207));
#134499=CARTESIAN_POINT('Ctrl Pts',(-20.2572650410679,21.2702062533114,
13.152227259641));
#134500=CARTESIAN_POINT('Ctrl Pts',(-20.1887611969922,21.3191608844268,
13.1563969739614));
#134501=CARTESIAN_POINT('Ctrl Pts',(-20.1180129698815,21.3646267316319,
13.1605666882818));
#134502=CARTESIAN_POINT('Ctrl Pts',(-20.0472672602965,21.410090960967,13.1647362542258));
#134503=CARTESIAN_POINT('Ctrl Pts',(-19.9742777139364,21.4520664052351,
13.1689058201699));
#134504=CARTESIAN_POINT('Ctrl Pts',(-19.8994263305452,21.4903379451218,
13.1730753861139));
#134505=CARTESIAN_POINT('Ctrl Pts',(-19.8219432648529,21.5299550651379,
13.1773915488528));
#134506=CARTESIAN_POINT('Ctrl Pts',(-19.7424654713779,21.5656027360311,
13.1817077115918));
#134507=CARTESIAN_POINT('Ctrl Pts',(-19.661441680213,21.5970955407954,13.1860238743307));
#134508=CARTESIAN_POINT('Ctrl Pts',(-19.5830572305233,21.6275624707569,
13.1901994385224));
#134509=CARTESIAN_POINT('Ctrl Pts',(-19.5032264199668,21.6541409631939,
13.194375002714));
#134510=CARTESIAN_POINT('Ctrl Pts',(-19.4223715061063,21.6767138255647,
13.1985505669057));
#134511=CARTESIAN_POINT('Ctrl Pts',(-19.3374328027607,21.700426789552,13.2029370289183));
#134512=CARTESIAN_POINT('Ctrl Pts',(-19.2513643920958,21.7197187126533,
13.2073234909308));
#134513=CARTESIAN_POINT('Ctrl Pts',(-19.1646662302712,21.734514731105,13.2117099529434));
#134514=CARTESIAN_POINT('Ctrl Pts',(-19.0779680684465,21.7493107495567,
13.2160964149559));
#134515=CARTESIAN_POINT('Ctrl Pts',(-18.9906407405948,21.7596108709354,
13.2204828769685));
#134516=CARTESIAN_POINT('Ctrl Pts',(-18.9031862415114,21.7654032601927,
13.224869338981));
#134517=CARTESIAN_POINT('Ctrl Pts',(-18.8197556535694,21.7709291330339,
13.2290539733741));
#134518=CARTESIAN_POINT('Ctrl Pts',(-18.735898795338,21.7723735414423,13.2332386077671));
#134519=CARTESIAN_POINT('Ctrl Pts',(-18.6520488590981,21.7696879470746,
13.2374232421602));
#134520=CARTESIAN_POINT('Ctrl Pts',(-18.568318272864,21.7670061753181,13.2416019202441));
#134521=CARTESIAN_POINT('Ctrl Pts',(-18.4845950449156,21.7602060920318,
13.2457805983281));
#134522=CARTESIAN_POINT('Ctrl Pts',(-18.4013160390446,21.749291035741,13.249959276412));
#134523=CARTESIAN_POINT('Ctrl Pts',(-18.3165443168449,21.7381803349106,
13.2542128542974));
#134524=CARTESIAN_POINT('Ctrl Pts',(-18.2322333798103,21.7228056564124,
13.2584664321829));
#134525=CARTESIAN_POINT('Ctrl Pts',(-18.1488425169103,21.7032260571594,
13.2627200100683));
#134526=CARTESIAN_POINT('Ctrl Pts',(-18.0670683486116,21.6840260466443,
13.2668911240463));
#134527=CARTESIAN_POINT('Ctrl Pts',(-17.9861793664179,21.660782811607,13.2710622380242));
#134528=CARTESIAN_POINT('Ctrl Pts',(-17.9066002780144,21.6336039090322,
13.2752333520022));
#134529=CARTESIAN_POINT('Ctrl Pts',(-17.8270478931424,21.6064341266006,
13.2794030663225));
#134530=CARTESIAN_POINT('Ctrl Pts',(-17.7488049640927,21.575331448026,13.2835727806429));
#134531=CARTESIAN_POINT('Ctrl Pts',(-17.6722807082307,21.5404531859398,
13.2877424949633));
#134532=CARTESIAN_POINT('Ctrl Pts',(-17.5957591754303,21.5055761649718,
13.2919120609073));
#134533=CARTESIAN_POINT('Ctrl Pts',(-17.5209566124703,21.466924019184,13.2960816268514));
#134534=CARTESIAN_POINT('Ctrl Pts',(-17.4482606698672,21.4247015099036,
13.3002511927954));
#134535=CARTESIAN_POINT('Ctrl Pts',(-17.3730088276023,21.3809945092841,
13.3045673555344));
#134536=CARTESIAN_POINT('Ctrl Pts',(-17.300014955555,21.3334616707481,13.3088835182733));
#134537=CARTESIAN_POINT('Ctrl Pts',(-17.2296778491729,21.282379942582,13.3131996810122));
#134538=CARTESIAN_POINT('Ctrl Pts',(-17.1616319666332,21.2329621963381,
13.3173752452039));
#134539=CARTESIAN_POINT('Ctrl Pts',(-17.0960727569881,21.180223552015,13.3215508093955));
#134540=CARTESIAN_POINT('Ctrl Pts',(-17.0333273206293,21.1244556272989,
13.3257263735872));
#134541=CARTESIAN_POINT('Ctrl Pts',(-16.9674127614429,21.065870997281,13.3301128355998));
#134542=CARTESIAN_POINT('Ctrl Pts',(-16.9046041088514,21.0039434366076,
13.3344992976123));
#134543=CARTESIAN_POINT('Ctrl Pts',(-16.8452349282194,20.939052806954,13.3388857596248));
#134544=CARTESIAN_POINT('Ctrl Pts',(-16.7858657475873,20.8741621773003,
13.3432722216374));
#134545=CARTESIAN_POINT('Ctrl Pts',(-16.7299363492651,20.8063089747714,
13.3476586836499));
#134546=CARTESIAN_POINT('Ctrl Pts',(-16.6777284049171,20.7359088914604,
13.3520451456625));
#134547=CARTESIAN_POINT('Ctrl Pts',(-16.6279226254793,20.6687480203406,
13.3562297800555));
#134548=CARTESIAN_POINT('Ctrl Pts',(-16.5813179797008,20.5990195040795,
13.3604144144486));
#134549=CARTESIAN_POINT('Ctrl Pts',(-16.5381897594128,20.527061315947,13.3645990488416));
#134550=CARTESIAN_POINT('Ctrl Pts',(-16.4951229268081,20.4552055513887,
13.3687777269256));
#134551=CARTESIAN_POINT('Ctrl Pts',(-16.4555229253635,20.3811268100632,
13.3729564050095));
#134552=CARTESIAN_POINT('Ctrl Pts',(-16.4196234139923,20.3051942323643,
13.3771350830935));
#134553=CARTESIAN_POINT('Ctrl Pts',(-16.3830804296802,20.2279006177819,
13.3813886609789));
#134554=CARTESIAN_POINT('Ctrl Pts',(-16.3503721900682,20.1486864403636,
13.3856422388643));
#134555=CARTESIAN_POINT('Ctrl Pts',(-16.3216976420463,20.0679698558357,
13.3898958167498));
#134556=CARTESIAN_POINT('Ctrl Pts',(-16.2935790060916,19.9888181198043,
13.3940669307277));
#134557=CARTESIAN_POINT('Ctrl Pts',(-16.2693392165557,19.9082221644555,
13.3982380447057));
#134558=CARTESIAN_POINT('Ctrl Pts',(-16.2491177212505,19.8265973202967,
13.4024091586836));
#134559=CARTESIAN_POINT('Ctrl Pts',(-16.2289030114633,19.7449998661427,
13.406578873004));
#134560=CARTESIAN_POINT('Ctrl Pts',(-16.2127040285388,19.6623746550205,
13.4107485873244));
#134561=CARTESIAN_POINT('Ctrl Pts',(-16.200609999048,19.579150924318,13.4149183016447));
#134562=CARTESIAN_POINT('Ctrl Pts',(-16.1885163999146,19.495930155073,13.4190878675888));
#134563=CARTESIAN_POINT('Ctrl Pts',(-16.1805275291,19.412111363967,13.4232574335328));
#134564=CARTESIAN_POINT('Ctrl Pts',(-16.1766810426044,19.3281313371599,
13.4274269994769));
#134565=CARTESIAN_POINT('Ctrl Pts',(-16.1726993183887,19.2411986762107,
13.4317431622158));
#134566=CARTESIAN_POINT('Ctrl Pts',(-16.1731567148618,19.1540937573817,
13.4360593249547));
#134567=CARTESIAN_POINT('Ctrl Pts',(-16.1780362227548,19.0673018113881,
13.4403754876936));
#134568=CARTESIAN_POINT('Ctrl Pts',(-16.1827567811914,18.9833371039063,
13.4445510518853));
#134569=CARTESIAN_POINT('Ctrl Pts',(-16.1916156782437,18.89966575566,13.448726616077));
#134570=CARTESIAN_POINT('Ctrl Pts',(-16.2045447628248,18.8167206534362,
13.4529021802687));
#134571=CARTESIAN_POINT('Ctrl Pts',(-16.218126864732,18.7295861912824,13.4572886422812));
#134572=CARTESIAN_POINT('Ctrl Pts',(-16.2362010106219,18.6432538400943,
13.4616751042937));
#134573=CARTESIAN_POINT('Ctrl Pts',(-16.2586283495453,18.5582096874759,
13.4660615663063));
#134574=CARTESIAN_POINT('Ctrl Pts',(-16.2810556884687,18.4731655348575,
13.4704480283188));
#134575=CARTESIAN_POINT('Ctrl Pts',(-16.3078359712665,18.3894101102965,
13.4748344903314));
#134576=CARTESIAN_POINT('Ctrl Pts',(-16.3387721302027,18.3074052613332,
13.4792209523439));
#134577=CARTESIAN_POINT('Ctrl Pts',(-16.3682827836177,18.2291791091759,
13.483405290821));
#134578=CARTESIAN_POINT('Ctrl Pts',(-16.4016845822185,18.1522546019467,
13.4875896292981));
#134579=CARTESIAN_POINT('Ctrl Pts',(-16.438842384669,18.0770460676078,13.4917739677752));
#134580=CARTESIAN_POINT('Ctrl Pts',(-16.4759497063905,18.0019397078159,
13.4959526216196));
#134581=CARTESIAN_POINT('Ctrl Pts',(-16.5168026975426,17.9285451005998,
13.5001312754641));
#134582=CARTESIAN_POINT('Ctrl Pts',(-16.5612174513678,17.857258519377,13.5043099293085));
#134583=CARTESIAN_POINT('Ctrl Pts',(-16.6055802939284,17.7860552567873,
13.5084836992082));
#134584=CARTESIAN_POINT('Ctrl Pts',(-16.653496382304,17.716955511052,13.5126574691079));
#134585=CARTESIAN_POINT('Ctrl Pts',(-16.7047357061378,17.6503314170985,
13.5168312390075));
#134586=CARTESIAN_POINT('Ctrl Pts',(-16.7559398356138,17.5837530847207,
13.5210021421022));
#134587=CARTESIAN_POINT('Ctrl Pts',(-16.8104623870111,17.5196473901113,
13.5251730451968));
#134588=CARTESIAN_POINT('Ctrl Pts',(-16.8680304516818,17.4583569545543,
13.5293439482914));
#134589=CARTESIAN_POINT('Ctrl Pts',(-16.9255842027832,17.397081758087,13.5335138143439));
#134590=CARTESIAN_POINT('Ctrl Pts',(-16.9861816530137,17.3386207695855,
13.5376836803963));
#134591=CARTESIAN_POINT('Ctrl Pts',(-17.0495108543087,17.2832820958324,
13.5418535464488));
#134592=CARTESIAN_POINT('Ctrl Pts',(-17.0900719874207,17.2478387416381,
13.5445242653045));
#134593=CARTESIAN_POINT('Ctrl Pts',(-17.1317529452028,17.2136754997451,
13.5471949841601));
#134594=CARTESIAN_POINT('Ctrl Pts',(-17.174464231106,17.180864983421,13.5498657030158));
#134595=CARTESIAN_POINT('Ctrl Pts',(-17.174464231106,17.180864983421,12.7499597594996));
#134596=CARTESIAN_POINT('Ctrl Pts',(-17.2410533408435,17.129711686913,12.7541315958235));
#134597=CARTESIAN_POINT('Ctrl Pts',(-17.3102192313192,17.0817939819445,
12.7583034321475));
#134598=CARTESIAN_POINT('Ctrl Pts',(-17.3816117456086,17.0373749151741,
12.7624752684715));
#134599=CARTESIAN_POINT('Ctrl Pts',(-17.4529733625773,16.9929750721301,
12.7666452993041));
#134600=CARTESIAN_POINT('Ctrl Pts',(-17.5265592997717,16.9520711033273,
12.7708153301367));
#134601=CARTESIAN_POINT('Ctrl Pts',(-17.6019903087145,16.9148828298984,
12.7749853609694));
#134602=CARTESIAN_POINT('Ctrl Pts',(-17.6774113001236,16.8776994952179,
12.7791548380056));
#134603=CARTESIAN_POINT('Ctrl Pts',(-17.7546764636973,16.844231078498,12.7833243150418));
#134604=CARTESIAN_POINT('Ctrl Pts',(-17.8333830590112,16.8146508756853,
12.787493792078));
#134605=CARTESIAN_POINT('Ctrl Pts',(-17.9121028115406,16.7850657280125,
12.7916639661169));
#134606=CARTESIAN_POINT('Ctrl Pts',(-17.9922640432294,16.7593702454841,
12.7958341401557));
#134607=CARTESIAN_POINT('Ctrl Pts',(-18.0734464975692,16.737688642644,12.8000043141946));
#134608=CARTESIAN_POINT('Ctrl Pts',(-18.1547182495494,16.7159831908578,
12.8041790752678));
#134609=CARTESIAN_POINT('Ctrl Pts',(-18.237013020941,16.6983005493885,12.808353836341));
#134610=CARTESIAN_POINT('Ctrl Pts',(-18.3198984700697,16.6847142040321,
12.8125285974141));
#134611=CARTESIAN_POINT('Ctrl Pts',(-18.4028355291097,16.6711193989268,
12.8167059579671));
#134612=CARTESIAN_POINT('Ctrl Pts',(-18.4863635411595,16.6616260185993,
12.82088331852));
#134613=CARTESIAN_POINT('Ctrl Pts',(-18.5700455072367,16.6562556048985,
12.825060679073));
#134614=CARTESIAN_POINT('Ctrl Pts',(-18.6538653038287,16.6508763457209,
12.8292449200541));
#134615=CARTESIAN_POINT('Ctrl Pts',(-18.7378391012384,16.6496336144523,
12.8334291610351));
#134616=CARTESIAN_POINT('Ctrl Pts',(-18.821530806815,16.6524968520914,12.8376134020162));
#134617=CARTESIAN_POINT('Ctrl Pts',(-18.859724062068,16.6538035092475,12.8395229076564));
#134618=CARTESIAN_POINT('Ctrl Pts',(-18.8978586532058,16.6559645670067,
12.8414324132965));
#134619=CARTESIAN_POINT('Ctrl Pts',(-18.9358937423124,16.6589735665916,
12.8433419189367));
#134620=CARTESIAN_POINT('Ctrl Pts',(-19.0192466995764,16.665567714777,12.8475265533297));
#134621=CARTESIAN_POINT('Ctrl Pts',(-19.1024313715334,16.6762620749485,
12.8517111877227));
#134622=CARTESIAN_POINT('Ctrl Pts',(-19.1850120996543,16.6910420467862,
12.8558958221158));
#134623=CARTESIAN_POINT('Ctrl Pts',(-19.2674752843302,16.7058009811635,
12.8600745001997));
#134624=CARTESIAN_POINT('Ctrl Pts',(-19.3493357837201,16.7246338957132,
12.8642531782837));
#134625=CARTESIAN_POINT('Ctrl Pts',(-19.4301618064486,16.7474743274644,
12.8684318563676));
#134626=CARTESIAN_POINT('Ctrl Pts',(-19.512436577546,16.7707241575396,12.872685434253));
#134627=CARTESIAN_POINT('Ctrl Pts',(-19.5936389405802,16.7981265494104,
12.8769390121385));
#134628=CARTESIAN_POINT('Ctrl Pts',(-19.6733229700782,16.8295566649858,
12.8811925900239));
#134629=CARTESIAN_POINT('Ctrl Pts',(-19.7514621691736,16.8603774464399,
12.8853637040019));
#134630=CARTESIAN_POINT('Ctrl Pts',(-19.8281409334341,16.8950709981003,
12.8895348179798));
#134631=CARTESIAN_POINT('Ctrl Pts',(-19.9029545672463,16.9334694909367,
12.8937059319578));
#134632=CARTESIAN_POINT('Ctrl Pts',(-19.9777430966213,16.9718550987881,
12.8978756462781));
#134633=CARTESIAN_POINT('Ctrl Pts',(-20.0506673295885,17.0139429688568,
12.9020453605985));
#134634=CARTESIAN_POINT('Ctrl Pts',(-20.1213450915266,17.0595182787165,
12.9062150749189));
#134635=CARTESIAN_POINT('Ctrl Pts',(-20.1920203384467,17.1050919668111,
12.910384640863));
#134636=CARTESIAN_POINT('Ctrl Pts',(-20.2604488871169,17.1541525979352,
12.914554206807));
#134637=CARTESIAN_POINT('Ctrl Pts',(-20.3262767630691,17.2064415174932,
12.9187237727511));
#134638=CARTESIAN_POINT('Ctrl Pts',(-20.3944190659323,17.2605688509573,
12.92303993549));
#134639=CARTESIAN_POINT('Ctrl Pts',(-20.45977400114,17.3181553818456,12.9273560982289));
#134640=CARTESIAN_POINT('Ctrl Pts',(-20.5219870028024,17.3788694157322,
12.9316722609678));
#134641=CARTESIAN_POINT('Ctrl Pts',(-20.5821734224794,17.4376056963509,
12.9358478251595));
#134642=CARTESIAN_POINT('Ctrl Pts',(-20.6394191762104,17.4992684748651,
12.9400233893512));
#134643=CARTESIAN_POINT('Ctrl Pts',(-20.6934427607506,17.5635219068703,
12.9441989535429));
#134644=CARTESIAN_POINT('Ctrl Pts',(-20.750194948117,17.6310206269781,12.9485854155554));
#134645=CARTESIAN_POINT('Ctrl Pts',(-20.8033905562332,17.7013781204558,
12.9529718775679));
#134646=CARTESIAN_POINT('Ctrl Pts',(-20.8527544426652,17.7741702913405,
12.9573583395805));
#134647=CARTESIAN_POINT('Ctrl Pts',(-20.9021183290971,17.8469624622252,
12.961744801593));
#134648=CARTESIAN_POINT('Ctrl Pts',(-20.9476502584794,17.922188774755,12.9661312636056));
#134649=CARTESIAN_POINT('Ctrl Pts',(-20.9891316170534,17.9993971815128,
12.9705177256181));
#134650=CARTESIAN_POINT('Ctrl Pts',(-21.030861876244,18.0770688619123,12.9749305077209));
#134651=CARTESIAN_POINT('Ctrl Pts',(-21.0686351706118,18.1570094498411,
12.9793432898236));
#134652=CARTESIAN_POINT('Ctrl Pts',(-21.1022126120114,18.2388019624017,
12.9837560719264));
#134653=CARTESIAN_POINT('Ctrl Pts',(-21.1356929152443,18.3203578525637,
12.9881560880307));
#134654=CARTESIAN_POINT('Ctrl Pts',(-21.1650014030465,18.4037546379829,
12.992556104135));
#134655=CARTESIAN_POINT('Ctrl Pts',(-21.1899457627446,18.4885524860192,
12.9969561202393));
#134656=CARTESIAN_POINT('Ctrl Pts',(-21.2148467487812,18.5732028861678,
13.0013484855235));
#134657=CARTESIAN_POINT('Ctrl Pts',(-21.2353985968836,18.6592491335648,
13.0057408508078));
#134658=CARTESIAN_POINT('Ctrl Pts',(-21.2514572537725,18.7462323425323,
13.010133216092));
#134659=CARTESIAN_POINT('Ctrl Pts',(-21.267478998332,18.8330156124333,13.0145154851125));
#134660=CARTESIAN_POINT('Ctrl Pts',(-21.2790280568695,18.9207311752703,
13.018897754133));
#134661=CARTESIAN_POINT('Ctrl Pts',(-21.28601069243,19.0089073833049,13.0232800231535));
#134662=CARTESIAN_POINT('Ctrl Pts',(-21.291327328341,19.0760454703582,13.0266167186811));
#134663=CARTESIAN_POINT('Ctrl Pts',(-21.2939976088987,19.1434502453364,
13.0299534142087));
#134664=CARTESIAN_POINT('Ctrl Pts',(-21.293999998394,19.2109093211998,13.0332901097364));
#134665=CARTESIAN_POINT('',(-21.2943302428071,19.2116425108278,12.9667098340901));
#134666=CARTESIAN_POINT('Ctrl Pts',(-17.1750494678687,17.181608263396,12.6831923912067));
#134667=CARTESIAN_POINT('Ctrl Pts',(-17.3565755014764,17.039342409566,12.6946551501856));
#134668=CARTESIAN_POINT('Ctrl Pts',(-18.295337787686,16.4863766829119,12.748509844725));
#134669=CARTESIAN_POINT('Ctrl Pts',(-20.4360629288883,16.7305239810473,
12.8430154491748));
#134670=CARTESIAN_POINT('Ctrl Pts',(-21.2952860172943,18.397872866616,12.9260582946456));
#134671=CARTESIAN_POINT('Ctrl Pts',(-21.2980344808449,19.2116308398979,
12.9667092045559));
#134672=CARTESIAN_POINT('Ctrl Pts',(-21.2939999191096,19.2116435515775,
12.9667098902285));
#134673=CARTESIAN_POINT('Ctrl Pts',(-21.2939911726516,19.2464363059257,
12.9684506873211));
#134674=CARTESIAN_POINT('Ctrl Pts',(-21.2932731600888,19.281219269613,12.9701914844137));
#134675=CARTESIAN_POINT('Ctrl Pts',(-21.2918468828523,19.3159729673895,
12.9719322815063));
#134676=CARTESIAN_POINT('Ctrl Pts',(-21.2884183105029,19.3995160291397,
12.9761169158993));
#134677=CARTESIAN_POINT('Ctrl Pts',(-21.2808860937369,19.4830464110296,
12.9803015502924));
#134678=CARTESIAN_POINT('Ctrl Pts',(-21.2692483017375,19.5661282142231,
12.9844861846854));
#134679=CARTESIAN_POINT('Ctrl Pts',(-21.2576270746945,19.6490917607532,
12.9886648627693));
#134680=CARTESIAN_POINT('Ctrl Pts',(-21.2419119432712,19.7316075451531,
12.9928435408533));
#134681=CARTESIAN_POINT('Ctrl Pts',(-21.2221529486456,19.8132415662722,
12.9970222189372));
#134682=CARTESIAN_POINT('Ctrl Pts',(-21.2020397882419,19.8963388185507,
13.0012757968227));
#134683=CARTESIAN_POINT('Ctrl Pts',(-21.1777363859676,19.9785219036746,
13.0055293747081));
#134684=CARTESIAN_POINT('Ctrl Pts',(-21.1493505801535,20.0593404829147,
13.0097829525936));
#134685=CARTESIAN_POINT('Ctrl Pts',(-21.1215150885756,20.1385922362917,
13.0139540665715));
#134686=CARTESIAN_POINT('Ctrl Pts',(-21.0897542310845,20.2165314648403,
13.0181251805494));
#134687=CARTESIAN_POINT('Ctrl Pts',(-21.0542203695085,20.292747399774,13.0222962945274));
#134688=CARTESIAN_POINT('Ctrl Pts',(-21.018698431663,20.3689377597145,13.0264660088478));
#134689=CARTESIAN_POINT('Ctrl Pts',(-20.9794061983923,20.4434055578918,
13.0306357231681));
#134690=CARTESIAN_POINT('Ctrl Pts',(-20.9365438451405,20.5157607482728,
13.0348054374885));
#134691=CARTESIAN_POINT('Ctrl Pts',(-20.8936830171152,20.5881133639457,
13.0389750034325));
#134692=CARTESIAN_POINT('Ctrl Pts',(-20.8472525568965,20.6583531259272,
13.0431445693766));
#134693=CARTESIAN_POINT('Ctrl Pts',(-20.7974975099507,20.7261165058923,
13.0473141353206));
#134694=CARTESIAN_POINT('Ctrl Pts',(-20.7459931369336,20.796262362702,13.0516302980595));
#134695=CARTESIAN_POINT('Ctrl Pts',(-20.6909263546122,20.8637540331552,
13.0559464607985));
#134696=CARTESIAN_POINT('Ctrl Pts',(-20.6326151733211,20.928224628182,13.0602626235374));
#134697=CARTESIAN_POINT('Ctrl Pts',(-20.5762034726275,20.9905951003567,
13.0644381877291));
#134698=CARTESIAN_POINT('Ctrl Pts',(-20.5167558657732,21.0501379976125,
13.0686137519207));
#134699=CARTESIAN_POINT('Ctrl Pts',(-20.4545972806998,21.1065592836016,
13.0727893161124));
#134700=CARTESIAN_POINT('Ctrl Pts',(-20.389299213262,21.1658302746175,13.077175778125));
#134701=CARTESIAN_POINT('Ctrl Pts',(-20.321009559389,21.2216556522273,13.0815622401375));
#134702=CARTESIAN_POINT('Ctrl Pts',(-20.2501416763133,21.2737443897259,
13.0859487021501));
#134703=CARTESIAN_POINT('Ctrl Pts',(-20.1792737932376,21.3258331272245,
13.0903351641626));
#134704=CARTESIAN_POINT('Ctrl Pts',(-20.1058282074104,21.3741849690991,
13.0947216261752));
#134705=CARTESIAN_POINT('Ctrl Pts',(-20.0302483510418,21.4185643167123,
13.0991080881878));
#134706=CARTESIAN_POINT('Ctrl Pts',(-19.9581460359011,21.4609017047557,
13.1032927225808));
#134707=CARTESIAN_POINT('Ctrl Pts',(-19.8838331576255,21.4997817138927,
13.1074773569739));
#134708=CARTESIAN_POINT('Ctrl Pts',(-19.8076751930389,21.5349667768393,
13.1116619913669));
#134709=CARTESIAN_POINT('Ctrl Pts',(-19.7316256298885,21.5701017582038,
13.1158406694508));
#134710=CARTESIAN_POINT('Ctrl Pts',(-19.6537366110357,21.6015520487103,
13.1200193475348));
#134711=CARTESIAN_POINT('Ctrl Pts',(-19.5744001491066,21.629124808479,13.1241980256187));
#134712=CARTESIAN_POINT('Ctrl Pts',(-19.4936416381155,21.6571917901503,
13.1284516035042));
#134713=CARTESIAN_POINT('Ctrl Pts',(-19.4113836985809,21.6812406201864,
13.1327051813896));
#134714=CARTESIAN_POINT('Ctrl Pts',(-19.3280633649498,21.701118213745,13.136958759275));
#134715=CARTESIAN_POINT('Ctrl Pts',(-19.2463583585722,21.7206104413645,
13.141129873253));
#134716=CARTESIAN_POINT('Ctrl Pts',(-19.1636322517455,21.7360916126581,
13.1453009872309));
#134717=CARTESIAN_POINT('Ctrl Pts',(-19.0803129065814,21.7474674984583,
13.1494721012089));
#134718=CARTESIAN_POINT('Ctrl Pts',(-18.9970215200283,21.7588395669701,
13.1536418155293));
#134719=CARTESIAN_POINT('Ctrl Pts',(-18.9131377459124,21.76610902368,13.1578115298496));
#134720=CARTESIAN_POINT('Ctrl Pts',(-18.8290979023926,21.7692330599381,
13.16198124417));
#134721=CARTESIAN_POINT('Ctrl Pts',(-18.7450610493711,21.7723569850297,
13.166150810114));
#134722=CARTESIAN_POINT('Ctrl Pts',(-18.6608685977348,21.7713357667235,
13.1703203760581));
#134723=CARTESIAN_POINT('Ctrl Pts',(-18.5769588557388,21.7661786784898,
13.1744899420021));
#134724=CARTESIAN_POINT('Ctrl Pts',(-18.4900989507281,21.7608402733958,
13.1788061047411));
#134725=CARTESIAN_POINT('Ctrl Pts',(-18.4035425318193,21.7510697851063,
13.18312226748));
#134726=CARTESIAN_POINT('Ctrl Pts',(-18.3177702276211,21.7369360198915,
13.1874384302189));
#134727=CARTESIAN_POINT('Ctrl Pts',(-18.2347919472104,21.7232626605919,
13.1916139944106));
#134728=CARTESIAN_POINT('Ctrl Pts',(-18.1525479314088,21.7055060719794,
13.1957895586022));
#134729=CARTESIAN_POINT('Ctrl Pts',(-18.0714612955845,21.6837803107335,
13.1999651227939));
#134730=CARTESIAN_POINT('Ctrl Pts',(-17.98627916655,21.6609572329353,13.2043515848065));
#134731=CARTESIAN_POINT('Ctrl Pts',(-17.9023749641124,21.6337536591884,
13.208738046819));
#134732=CARTESIAN_POINT('Ctrl Pts',(-17.8202171381048,21.6023596302745,
13.2131245088315));
#134733=CARTESIAN_POINT('Ctrl Pts',(-17.7380593120971,21.5709656013606,
13.2175109708441));
#134734=CARTESIAN_POINT('Ctrl Pts',(-17.6576483623233,21.5353814216376,
13.2218974328566));
#134735=CARTESIAN_POINT('Ctrl Pts',(-17.579422411398,21.4958524223455,13.2262838948691));
#134736=CARTESIAN_POINT('Ctrl Pts',(-17.5047957524334,21.4581422109068,
13.2304685292622));
#134737=CARTESIAN_POINT('Ctrl Pts',(-17.4318796660886,21.4167018520732,
13.2346531636552));
#134738=CARTESIAN_POINT('Ctrl Pts',(-17.3610717345268,21.3717100633506,
13.2388377980483));
#134739=CARTESIAN_POINT('Ctrl Pts',(-17.2903645892912,21.3267823148704,
13.2430164761322));
#134740=CARTESIAN_POINT('Ctrl Pts',(-17.2217600234686,21.2783134219689,
13.2471951542162));
#134741=CARTESIAN_POINT('Ctrl Pts',(-17.1556323738797,21.2265286246579,
13.2513738323001));
#134742=CARTESIAN_POINT('Ctrl Pts',(-17.0883194336969,21.173815622072,13.2556274101856));
#134743=CARTESIAN_POINT('Ctrl Pts',(-17.0235735109216,21.117666888101,13.259880988071));
#134744=CARTESIAN_POINT('Ctrl Pts',(-16.9617598841366,21.0583670376307,
13.2641345659564));
#134745=CARTESIAN_POINT('Ctrl Pts',(-16.9011446351263,21.000216830476,13.2683056799344));
#134746=CARTESIAN_POINT('Ctrl Pts',(-16.8433493474163,20.9390369307226,
13.2724767939123));
#134747=CARTESIAN_POINT('Ctrl Pts',(-16.7886848464703,20.8751360982347,
13.2766479078903));
#134748=CARTESIAN_POINT('Ctrl Pts',(-16.7340386887256,20.8112567082883,
13.2808176222107));
#134749=CARTESIAN_POINT('Ctrl Pts',(-16.6825215301017,20.7446585481929,
13.284987336531));
#134750=CARTESIAN_POINT('Ctrl Pts',(-16.6344055366424,20.6756853209608,
13.2891570508514));
#134751=CARTESIAN_POINT('Ctrl Pts',(-16.5862912553567,20.6067145480922,
13.2933266167954));
#134752=CARTESIAN_POINT('Ctrl Pts',(-16.5415781611063,20.5353692539102,
13.2974961827395));
#134753=CARTESIAN_POINT('Ctrl Pts',(-16.5004957043155,20.4620230058472,
13.3016657486835));
#134754=CARTESIAN_POINT('Ctrl Pts',(-16.4579688390247,20.3860979941846,
13.3059819114225));
#134755=CARTESIAN_POINT('Ctrl Pts',(-16.4193329255797,20.3080291637333,
13.3102980741614));
#134756=CARTESIAN_POINT('Ctrl Pts',(-16.3847902639464,20.2282578906211,
13.3146142369003));
#134757=CARTESIAN_POINT('Ctrl Pts',(-16.3513728258826,20.1510851583402,
13.318789801092));
#134758=CARTESIAN_POINT('Ctrl Pts',(-16.3217861809924,20.0723196518131,
13.3229653652837));
#134759=CARTESIAN_POINT('Ctrl Pts',(-16.2961634499818,19.9923788808225,
13.3271409294753));
#134760=CARTESIAN_POINT('Ctrl Pts',(-16.2692465757402,19.9084004915302,
13.3315273914879));
#134761=CARTESIAN_POINT('Ctrl Pts',(-16.246704722792,19.8231255568952,13.3359138535004));
#134762=CARTESIAN_POINT('Ctrl Pts',(-16.2286316599242,19.7370508345642,
13.340300315513));
#134763=CARTESIAN_POINT('Ctrl Pts',(-16.2105585970564,19.6509761122332,
13.3446867775255));
#134764=CARTESIAN_POINT('Ctrl Pts',(-16.1969543388866,19.5641021872051,
13.3490732395381));
#134765=CARTESIAN_POINT('Ctrl Pts',(-16.1878497481282,19.4769302444118,
13.3534597015506));
#134766=CARTESIAN_POINT('Ctrl Pts',(-16.1791640730867,19.3937692119263,
13.3576443359437));
#134767=CARTESIAN_POINT('Ctrl Pts',(-16.1745407622114,19.3100274422731,
13.3618289703367));
#134768=CARTESIAN_POINT('Ctrl Pts',(-16.1740447460464,19.2261359755289,
13.3660136047298));
#134769=CARTESIAN_POINT('Ctrl Pts',(-16.173549435899,19.1423639179039,13.3701922828137));
#134770=CARTESIAN_POINT('Ctrl Pts',(-16.1771697541693,19.0584430425126,
13.3743709608977));
#134771=CARTESIAN_POINT('Ctrl Pts',(-16.1849189310737,18.9748100255276,
13.3785496389816));
#134772=CARTESIAN_POINT('Ctrl Pts',(-16.1928070064048,18.8896779468192,
13.382803216867));
#134773=CARTESIAN_POINT('Ctrl Pts',(-16.2049734659499,18.804844627276,13.3870567947525));
#134774=CARTESIAN_POINT('Ctrl Pts',(-16.2213767120001,18.7207712650195,
13.3913103726379));
#134775=CARTESIAN_POINT('Ctrl Pts',(-16.2374619491174,18.6383278289459,
13.3954814866159));
#134776=CARTESIAN_POINT('Ctrl Pts',(-16.2576210698179,18.5566156189164,
13.3996526005938));
#134777=CARTESIAN_POINT('Ctrl Pts',(-16.2817626998464,18.4760631158151,
13.4038237145718));
#134778=CARTESIAN_POINT('Ctrl Pts',(-16.3058962289179,18.3955376428842,
13.4079934288921));
#134779=CARTESIAN_POINT('Ctrl Pts',(-16.3340094813079,18.3161715443229,
13.4121631432125));
#134780=CARTESIAN_POINT('Ctrl Pts',(-16.3659607754927,18.2383797086247,
13.4163328575329));
#134781=CARTESIAN_POINT('Ctrl Pts',(-16.3979109327134,18.1605906410939,
13.4205024234769));
#134782=CARTESIAN_POINT('Ctrl Pts',(-16.4336986846161,18.0843761502596,
13.424671989421));
#134783=CARTESIAN_POINT('Ctrl Pts',(-16.4731341172713,18.0101313725834,
13.428841555365));
#134784=CARTESIAN_POINT('Ctrl Pts',(-16.5139560510898,17.933276240115,13.433157718104));
#134785=CARTESIAN_POINT('Ctrl Pts',(-16.5586866956794,17.8585323739429,
13.4374738808429));
#134786=CARTESIAN_POINT('Ctrl Pts',(-16.6070644247003,17.7863087848504,
13.4417900435818));
#134787=CARTESIAN_POINT('Ctrl Pts',(-16.6538662542868,17.7164378715759,
13.4459656077735));
#134788=CARTESIAN_POINT('Ctrl Pts',(-16.7040808906405,17.6489259106341,
13.4501411719652));
#134789=CARTESIAN_POINT('Ctrl Pts',(-16.7574293298199,17.5841108255988,
13.4543167361568));
#134790=CARTESIAN_POINT('Ctrl Pts',(-16.8134722718384,17.5160220847016,
13.4587031981694));
#134791=CARTESIAN_POINT('Ctrl Pts',(-16.8729735193545,17.450910248947,13.4630896601819));
#134792=CARTESIAN_POINT('Ctrl Pts',(-16.9355661330671,17.3891230485379,
13.4674761221945));
#134793=CARTESIAN_POINT('Ctrl Pts',(-16.9981587467797,17.3273358481289,
13.471862584207));
#134794=CARTESIAN_POINT('Ctrl Pts',(-17.0638422427094,17.2688736120054,
13.4762490462195));
#134795=CARTESIAN_POINT('Ctrl Pts',(-17.1322119090441,17.2140335727229,
13.4806355082321));
#134796=CARTESIAN_POINT('Ctrl Pts',(-17.1461740369508,17.2028344008691,
13.4815312906303));
#134797=CARTESIAN_POINT('Ctrl Pts',(-17.1602591664528,17.1917772164721,
13.4824270730286));
#134798=CARTESIAN_POINT('Ctrl Pts',(-17.174464231106,17.180864983421,13.4833228554268));
#134799=CARTESIAN_POINT('Origin',(-18.734,19.211,-1.76670989022852));
#134800=CARTESIAN_POINT('',(-17.1732300624786,17.1792869614928,14.3497865218036));
#134801=CARTESIAN_POINT('',(-17.1756294966408,17.182412846113,14.2834124313123));
#134802=CARTESIAN_POINT('',(-17.174464231106,17.180864983421,-1.76670989022852));
#134803=CARTESIAN_POINT('',(-21.2939989424941,19.2133268925441,13.8332901097715));
#134804=CARTESIAN_POINT('Ctrl Pts',(-21.2944497455462,19.2133273022983,
13.8332901097715));
#134805=CARTESIAN_POINT('Ctrl Pts',(-21.2961552640167,19.3972186594194,
13.8424428639771));
#134806=CARTESIAN_POINT('Ctrl Pts',(-21.1940977855363,20.4309438993384,
13.8939875537431));
#134807=CARTESIAN_POINT('Ctrl Pts',(-19.7898863418736,22.047969473252,13.9879241790696));
#134808=CARTESIAN_POINT('Ctrl Pts',(-16.9200888835355,21.634431084369,14.1150999857511));
#134809=CARTESIAN_POINT('Ctrl Pts',(-15.7765849628929,19.1334581710982,
14.2357207666624));
#134810=CARTESIAN_POINT('Ctrl Pts',(-16.6072658097655,17.6225945609841,
14.3139496120132));
#134811=CARTESIAN_POINT('Ctrl Pts',(-17.1732300624786,17.1792869614928,
14.3497865218036));
#134812=CARTESIAN_POINT('Ctrl Pts',(-17.174464231106,17.180864983421,13.5498657030158));
#134813=CARTESIAN_POINT('Ctrl Pts',(-17.2411543251493,17.1296341114632,
13.5540358067222));
#134814=CARTESIAN_POINT('Ctrl Pts',(-17.3103576653337,17.0817034418445,
13.5582059104285));
#134815=CARTESIAN_POINT('Ctrl Pts',(-17.3817086482351,17.0373146271961,
13.5623760141349));
#134816=CARTESIAN_POINT('Ctrl Pts',(-17.4531374462619,16.9928774022659,
13.5665506657413));
#134817=CARTESIAN_POINT('Ctrl Pts',(-17.5267181707769,16.9519899856981,
13.5707253173478));
#134818=CARTESIAN_POINT('Ctrl Pts',(-17.6020588076407,16.914849060484,13.5748999689542));
#134819=CARTESIAN_POINT('Ctrl Pts',(-17.677445250084,16.8776855543405,13.5790771586642));
#134820=CARTESIAN_POINT('Ctrl Pts',(-17.7545933127803,16.8442732563227,
13.5832543483742));
#134821=CARTESIAN_POINT('Ctrl Pts',(-17.8330913235602,16.8147605385281,
13.5874315380842));
#134822=CARTESIAN_POINT('Ctrl Pts',(-17.9117198950076,16.7851987341374,
13.5916156754438));
#134823=CARTESIAN_POINT('Ctrl Pts',(-17.9917024590505,16.7595495978572,
13.5957998128035));
#134824=CARTESIAN_POINT('Ctrl Pts',(-18.0726129198988,16.7379114188377,
13.5999839501631));
#134825=CARTESIAN_POINT('Ctrl Pts',(-18.1139486661373,16.7268568497791,
13.6021215531172));
#134826=CARTESIAN_POINT('Ctrl Pts',(-18.1555264377626,16.7168483177079,
13.6042591560712));
#134827=CARTESIAN_POINT('Ctrl Pts',(-18.1972887614196,16.7078937205182,
13.6063967590253));
#134828=CARTESIAN_POINT('Ctrl Pts',(-18.2790439141133,16.6903639377749,
13.6105813934184));
#134829=CARTESIAN_POINT('Ctrl Pts',(-18.3618109357873,16.6768111110841,
13.6147660278114));
#134830=CARTESIAN_POINT('Ctrl Pts',(-18.4451682027609,16.6673458975514,
13.6189506622045));
#134831=CARTESIAN_POINT('Ctrl Pts',(-18.5284068209824,16.6578941565787,
13.6231293402884));
#134832=CARTESIAN_POINT('Ctrl Pts',(-18.6122335625328,16.6525185234246,
13.6273080183723));
#134833=CARTESIAN_POINT('Ctrl Pts',(-18.6962156707035,16.6512788541602,
13.6314866964563));
#134834=CARTESIAN_POINT('Ctrl Pts',(-18.7817030978064,16.6500169647151,
13.6357402743417));
#134835=CARTESIAN_POINT('Ctrl Pts',(-18.867351044784,16.6530408729659,13.6399938522271));
#134836=CARTESIAN_POINT('Ctrl Pts',(-18.9526965098734,16.6603585440974,
13.6442474301126));
#134837=CARTESIAN_POINT('Ctrl Pts',(-19.036387386584,16.6675343478947,13.6484185440905));
#134838=CARTESIAN_POINT('Ctrl Pts',(-19.1197869256877,16.6788388732103,
13.6525896580685));
#134839=CARTESIAN_POINT('Ctrl Pts',(-19.2024593314997,16.6942270951214,
13.6567607720464));
#134840=CARTESIAN_POINT('Ctrl Pts',(-19.2851039957874,16.7096101533661,
13.6609304863668));
#134841=CARTESIAN_POINT('Ctrl Pts',(-19.3670215594759,16.729074102609,13.6651002006872));
#134842=CARTESIAN_POINT('Ctrl Pts',(-19.4477843610407,16.7525224455095,
13.6692699150076));
#134843=CARTESIAN_POINT('Ctrl Pts',(-19.5285442887184,16.7759699540173,
13.6734394809516));
#134844=CARTESIAN_POINT('Ctrl Pts',(-19.6081490944211,16.8034014451982,
13.6776090468957));
#134845=CARTESIAN_POINT('Ctrl Pts',(-19.6861855970009,16.8346703534938,
13.6817786128397));
#134846=CARTESIAN_POINT('Ctrl Pts',(-19.766965766743,16.8670386380308,13.6860947755786));
#134847=CARTESIAN_POINT('Ctrl Pts',(-19.8460648087822,16.9035190114424,
13.6904109383175));
#134848=CARTESIAN_POINT('Ctrl Pts',(-19.9230480777099,16.9438950908936,
13.6947271010565));
#134849=CARTESIAN_POINT('Ctrl Pts',(-19.9975236247495,16.9829559238035,
13.6989026652482));
#134850=CARTESIAN_POINT('Ctrl Pts',(-20.0700187425844,17.0256622753738,
13.7030782294398));
#134851=CARTESIAN_POINT('Ctrl Pts',(-20.140167606798,17.0717728821857,13.7072537936315));
#134852=CARTESIAN_POINT('Ctrl Pts',(-20.21385952338,17.1202124261301,13.7116402556441));
#134853=CARTESIAN_POINT('Ctrl Pts',(-20.2849614681662,17.1724088154587,
13.7160267176566));
#134854=CARTESIAN_POINT('Ctrl Pts',(-20.3530884618266,17.2280344045395,
13.7204131796692));
#134855=CARTESIAN_POINT('Ctrl Pts',(-20.421215455487,17.2836599936203,13.7247996416817));
#134856=CARTESIAN_POINT('Ctrl Pts',(-20.4863671192073,17.3427143364292,
13.7291861036942));
#134857=CARTESIAN_POINT('Ctrl Pts',(-20.548204641978,17.4048268308311,13.7335725657068));
#134858=CARTESIAN_POINT('Ctrl Pts',(-20.6067777194386,17.4636603639817,
13.7377274633762));
#134859=CARTESIAN_POINT('Ctrl Pts',(-20.6626103382647,17.5254713783546,
13.7418823610455));
#134860=CARTESIAN_POINT('Ctrl Pts',(-20.7153787245625,17.5899699725634,
13.7460372587149));
#134861=CARTESIAN_POINT('Ctrl Pts',(-20.7677053791601,17.6539286398258,
13.7501573751423));
#134862=CARTESIAN_POINT('Ctrl Pts',(-20.8170185699061,17.7205297194409,
13.7542774915697));
#134863=CARTESIAN_POINT('Ctrl Pts',(-20.8630375889925,17.7894519196816,
13.7583976079971));
#134864=CARTESIAN_POINT('Ctrl Pts',(-20.9090125260321,17.8583080987051,
13.7625137777266));
#134865=CARTESIAN_POINT('Ctrl Pts',(-20.951699290088,17.9294805955782,13.7666299474561));
#134866=CARTESIAN_POINT('Ctrl Pts',(-20.9908578231797,18.0026156381546,
13.7707461171856));
#134867=CARTESIAN_POINT('Ctrl Pts',(-21.0299913601116,18.0757039962649,
13.7748596594307));
#134868=CARTESIAN_POINT('Ctrl Pts',(-21.0656009133711,18.1507519968574,
13.7789732016758));
#134869=CARTESIAN_POINT('Ctrl Pts',(-21.0974909394082,18.2273788435911,
13.7830867439209));
#134870=CARTESIAN_POINT('Ctrl Pts',(-21.1299241917558,18.3053109799219,
13.7872703577417));
#134871=CARTESIAN_POINT('Ctrl Pts',(-21.1585097661409,18.3848758167557,
13.7914539715626));
#134872=CARTESIAN_POINT('Ctrl Pts',(-21.1830923574767,18.4656499986255,
13.7956375853835));
#134873=CARTESIAN_POINT('Ctrl Pts',(-21.2072638620762,18.5450734199364,
13.7997512379815));
#134874=CARTESIAN_POINT('Ctrl Pts',(-21.2275651518659,18.6256655681997,
13.8038648905795));
#134875=CARTESIAN_POINT('Ctrl Pts',(-21.2438990336338,18.7070090864272,
13.8079785431775));
#134876=CARTESIAN_POINT('Ctrl Pts',(-21.260649602877,18.7904277283589,13.8121971376098));
#134877=CARTESIAN_POINT('Ctrl Pts',(-21.2732274574716,18.8746360871023,
13.8164157320421));
#134878=CARTESIAN_POINT('Ctrl Pts',(-21.2815840465261,18.9591756050627,
13.8206343264745));
#134879=CARTESIAN_POINT('Ctrl Pts',(-21.2899406355806,19.043715123023,13.8248529209068));
#134880=CARTESIAN_POINT('Ctrl Pts',(-21.2940759677847,19.1285852645553,
13.8290715153392));
#134881=CARTESIAN_POINT('Ctrl Pts',(-21.2939989424941,19.2133268925441,
13.8332901097715));
#134882=CARTESIAN_POINT('',(-21.2939989173812,19.2086456408557,13.7667098774912));
#134883=CARTESIAN_POINT('Ctrl Pts',(-17.174464231106,17.180864983421,13.4833228554268));
#134884=CARTESIAN_POINT('Ctrl Pts',(-17.2408009142214,17.1299055993094,
13.4875060981324));
#134885=CARTESIAN_POINT('Ctrl Pts',(-17.3097560410181,17.0821103414713,
13.4916893408381));
#134886=CARTESIAN_POINT('Ctrl Pts',(-17.3809949048231,17.0377588232262,
13.4958725835437));
#134887=CARTESIAN_POINT('Ctrl Pts',(-17.4521374194886,16.993467289523,13.5000501684971));
#134888=CARTESIAN_POINT('Ctrl Pts',(-17.5255571481475,16.9526104846787,
13.5042277534506));
#134889=CARTESIAN_POINT('Ctrl Pts',(-17.6008877396761,16.9154267370647,
13.508405338404));
#134890=CARTESIAN_POINT('Ctrl Pts',(-17.6761383840039,16.8782824519914,
13.5125784897507));
#134891=CARTESIAN_POINT('Ctrl Pts',(-17.7532954499436,16.8448036790587,
13.5167516410973));
#134892=CARTESIAN_POINT('Ctrl Pts',(-17.8319663255885,16.8151838029123,
13.520924792444));
#134893=CARTESIAN_POINT('Ctrl Pts',(-17.9105918009404,16.7855810201445,
13.5250955355005));
#134894=CARTESIAN_POINT('Ctrl Pts',(-17.9907289220234,16.7598328745479,
13.529266278557));
#134895=CARTESIAN_POINT('Ctrl Pts',(-18.0719643826269,16.7380849506444,
13.5334370216135));
#134896=CARTESIAN_POINT('Ctrl Pts',(-18.1531773319184,16.7163430533492,
13.5376066089076));
#134897=CARTESIAN_POINT('Ctrl Pts',(-18.2354875720585,16.6985992948508,
13.5417761962016));
#134898=CARTESIAN_POINT('Ctrl Pts',(-18.3184672066022,16.6849492290116,
13.5459457834956));
#134899=CARTESIAN_POINT('Ctrl Pts',(-18.4014487382646,16.6712988510983,
13.5501154661167));
#134900=CARTESIAN_POINT('Ctrl Pts',(-18.4850992405653,16.6617424250825,
13.5542851487377));
#134901=CARTESIAN_POINT('Ctrl Pts',(-18.5689825669994,16.6563240427002,
13.5584548313588));
#134902=CARTESIAN_POINT('Ctrl Pts',(-18.6529509714077,16.650900164768,13.5626287430462));
#134903=CARTESIAN_POINT('Ctrl Pts',(-18.7371522114986,16.6496227435834,
13.5668026547335));
#134904=CARTESIAN_POINT('Ctrl Pts',(-18.8211474534948,16.6524837656663,
13.5709765664209));
#134905=CARTESIAN_POINT('Ctrl Pts',(-18.9051841270904,16.6553461989804,
13.5751525369372));
#134906=CARTESIAN_POINT('Ctrl Pts',(-18.9890141412379,16.6623511034493,
13.5793285074536));
#134907=CARTESIAN_POINT('Ctrl Pts',(-19.0722035617808,16.6734385030509,
13.5835044779699));
#134908=CARTESIAN_POINT('Ctrl Pts',(-19.1555423768616,16.6845458138013,
13.5876879478435));
#134909=CARTESIAN_POINT('Ctrl Pts',(-19.2382378461903,16.6997501856857,
13.5918714177171));
#134910=CARTESIAN_POINT('Ctrl Pts',(-19.3198660896852,16.7189404250787,
13.5960548875907));
#134911=CARTESIAN_POINT('Ctrl Pts',(-19.3963302483165,16.736916623589,13.5999736966983));
#134912=CARTESIAN_POINT('Ctrl Pts',(-19.471857774533,16.7583897384897,13.6038925058059));
#134913=CARTESIAN_POINT('Ctrl Pts',(-19.5461152252309,16.783229652346,13.6078113149135));
#134914=CARTESIAN_POINT('Ctrl Pts',(-19.6254097949838,16.809754536562,13.6119959493065));
#134915=CARTESIAN_POINT('Ctrl Pts',(-19.7035510491552,16.8402176845382,
13.6161805836996));
#134916=CARTESIAN_POINT('Ctrl Pts',(-19.7801197445754,16.8744997367838,
13.6203652180926));
#134917=CARTESIAN_POINT('Ctrl Pts',(-19.856579453935,16.9087329927713,13.6245438961766));
#134918=CARTESIAN_POINT('Ctrl Pts',(-19.9314706343179,16.9467741695628,
13.6287225742605));
#134919=CARTESIAN_POINT('Ctrl Pts',(-20.0043903176931,16.9884545132413,
13.6329012523445));
#134920=CARTESIAN_POINT('Ctrl Pts',(-20.0786170339864,17.0308819471251,
13.6371548302299));
#134921=CARTESIAN_POINT('Ctrl Pts',(-20.1508004226817,17.0770801423177,
13.6414084081153));
#134922=CARTESIAN_POINT('Ctrl Pts',(-20.2205378947047,17.1268202842349,
13.6456619860008));
#134923=CARTESIAN_POINT('Ctrl Pts',(-20.288923369751,17.1755961164411,13.6498330999787));
#134924=CARTESIAN_POINT('Ctrl Pts',(-20.3549565277687,17.2277775063951,
13.6540042139567));
#134925=CARTESIAN_POINT('Ctrl Pts',(-20.4182851699542,17.283103875653,13.6581753279346));
#134926=CARTESIAN_POINT('Ctrl Pts',(-20.4815925616022,17.3384116796133,
13.662345042255));
#134927=CARTESIAN_POINT('Ctrl Pts',(-20.5421968936246,17.3968620645641,
13.6665147565753));
#134928=CARTESIAN_POINT('Ctrl Pts',(-20.5997791685761,17.4581542868503,
13.6706844708957));
#134929=CARTESIAN_POINT('Ctrl Pts',(-20.6573593945032,17.5194443280962,
13.6748540368398));
#134930=CARTESIAN_POINT('Ctrl Pts',(-20.7119174628062,17.5835756697508,
13.6790236027838));
#134931=CARTESIAN_POINT('Ctrl Pts',(-20.763172325239,17.6502118418939,13.6831931687278));
#134932=CARTESIAN_POINT('Ctrl Pts',(-20.8162292454052,17.719190859645,13.6875093314668));
#134933=CARTESIAN_POINT('Ctrl Pts',(-20.8657460348867,17.79085370675,13.6918254942057));
#134934=CARTESIAN_POINT('Ctrl Pts',(-20.911458707217,17.864792891727,13.6961416569446));
#134935=CARTESIAN_POINT('Ctrl Pts',(-20.9556822940543,17.9363235155303,
13.7003172211363));
#134936=CARTESIAN_POINT('Ctrl Pts',(-20.9963456096572,18.0099840160616,
13.704492785328));
#134937=CARTESIAN_POINT('Ctrl Pts',(-21.0332565704859,18.0853805158591,
13.7086683495196));
#134938=CARTESIAN_POINT('Ctrl Pts',(-21.0720318161985,18.1645851136233,
13.7130548115322));
#134939=CARTESIAN_POINT('Ctrl Pts',(-21.1066654530387,18.245705153136,13.7174412735447));
#134940=CARTESIAN_POINT('Ctrl Pts',(-21.1369928787006,18.3282626523623,
13.7218277355573));
#134941=CARTESIAN_POINT('Ctrl Pts',(-21.1673203043624,18.4108201515887,
13.7262141975698));
#134942=CARTESIAN_POINT('Ctrl Pts',(-21.1933414198056,18.494814533789,13.7306006595824));
#134943=CARTESIAN_POINT('Ctrl Pts',(-21.214953227824,18.5797543415201,13.7349871215949));
#134944=CARTESIAN_POINT('Ctrl Pts',(-21.2416966549181,18.6848626949492,
13.740415127754));
#134945=CARTESIAN_POINT('Ctrl Pts',(-21.2617718479477,18.7917315462695,
13.7458431339131));
#134946=CARTESIAN_POINT('Ctrl Pts',(-21.2749934581325,18.8996284442541,
13.7512711400722));
#134947=CARTESIAN_POINT('Ctrl Pts',(-21.2875287526721,19.0019245622934,
13.7564173858785));
#134948=CARTESIAN_POINT('Ctrl Pts',(-21.2939037306914,19.1051449394058,
13.7615636316849));
#134949=CARTESIAN_POINT('Ctrl Pts',(-21.2939989173812,19.2086456408557,
13.7667098774912));
#134950=CARTESIAN_POINT('Ctrl Pts',(-21.2935817003363,19.2086462806877,
13.7667098902285));
#134951=CARTESIAN_POINT('Ctrl Pts',(-21.2877698482561,19.8484613719781,
13.7985275695778));
#134952=CARTESIAN_POINT('Ctrl Pts',(-20.7208250258792,21.3499116215441,
13.8727371844875));
#134953=CARTESIAN_POINT('Ctrl Pts',(-18.1988330521628,22.1904106768542,
13.9893387349578));
#134954=CARTESIAN_POINT('Ctrl Pts',(-15.9391114041072,20.373707779263,14.1165145416392));
#134955=CARTESIAN_POINT('Ctrl Pts',(-16.1737485207935,18.1512291376149,
14.2145391070908));
#134956=CARTESIAN_POINT('Ctrl Pts',(-16.9627571498223,17.3430212960427,
14.2701717369818));
#134957=CARTESIAN_POINT('Ctrl Pts',(-17.1756294966411,17.1824128461128,
14.2834124313123));
#134958=CARTESIAN_POINT('Origin',(-18.734,19.211,-1.76670989022852));
#134959=CARTESIAN_POINT('',(-17.174464231106,17.180864983421,15.149955384767));
#134960=CARTESIAN_POINT('',(-17.174464231106,17.180864983421,15.0832685841393));
#134961=CARTESIAN_POINT('',(-17.174464231106,17.180864983421,-1.76670989022852));
#134962=CARTESIAN_POINT('',(-21.2941234937244,19.2098698166564,14.6332901097715));
#134963=CARTESIAN_POINT('Ctrl Pts',(-21.2939997505486,19.2098698712836,
14.6332901097715));
#134964=CARTESIAN_POINT('Ctrl Pts',(-21.2940362985033,19.2926593390013,
14.6374299052976));
#134965=CARTESIAN_POINT('Ctrl Pts',(-21.2900525381051,19.3756125071059,
14.6415697008237));
#134966=CARTESIAN_POINT('Ctrl Pts',(-21.2820270867845,19.4583013647603,
14.6457094963498));
#134967=CARTESIAN_POINT('Ctrl Pts',(-21.2740124509524,19.5408787868902,
14.6498437128862));
#134968=CARTESIAN_POINT('Ctrl Pts',(-21.2619669829652,19.623192141297,14.6539779294226));
#134969=CARTESIAN_POINT('Ctrl Pts',(-21.2459213201026,19.7048130026779,
14.658112145959));
#134970=CARTESIAN_POINT('Ctrl Pts',(-21.2298921267197,19.7863500873319,
14.6622421190811));
#134971=CARTESIAN_POINT('Ctrl Pts',(-21.209870984755,19.8671956313595,14.6663720922032));
#134972=CARTESIAN_POINT('Ctrl Pts',(-21.1859402178855,19.9469274202771,
14.6705020653253));
#134973=CARTESIAN_POINT('Ctrl Pts',(-21.1620224032908,20.026616055206,14.6746298031431));
#134974=CARTESIAN_POINT('Ctrl Pts',(-21.1341992976676,20.105191681447,14.6787575409609));
#134975=CARTESIAN_POINT('Ctrl Pts',(-21.1026037847566,20.1822446194635,
14.6828852787786));
#134976=CARTESIAN_POINT('Ctrl Pts',(-21.0710154147152,20.2592801379466,
14.6870120834293));
#134977=CARTESIAN_POINT('Ctrl Pts',(-21.0356565094082,20.3347932165768,
14.69113888808));
#134978=CARTESIAN_POINT('Ctrl Pts',(-20.9967085276621,20.4083930511094,
14.6952656927306));
#134979=CARTESIAN_POINT('Ctrl Pts',(-20.9577570758468,20.481999443017,14.6993928650588));
#134980=CARTESIAN_POINT('Ctrl Pts',(-20.915216134864,20.5536918375766,14.703520037387));
#134981=CARTESIAN_POINT('Ctrl Pts',(-20.8693129406042,20.6231043324372,
14.7076472097152));
#134982=CARTESIAN_POINT('Ctrl Pts',(-20.82336222789,20.6925886823078,14.7117786544443));
#134983=CARTESIAN_POINT('Ctrl Pts',(-20.7740425759679,20.7597880294049,
14.7159100991735));
#134984=CARTESIAN_POINT('Ctrl Pts',(-20.7216239583874,20.8243663564251,
14.7200415439026));
#134985=CARTESIAN_POINT('Ctrl Pts',(-20.6691749218121,20.8889821588287,
14.7241753861462));
#134986=CARTESIAN_POINT('Ctrl Pts',(-20.6136236562298,20.9509735655346,
14.7283092283899));
#134987=CARTESIAN_POINT('Ctrl Pts',(-20.5552780488243,21.0100403744415,
14.7324430706335));
#134988=CARTESIAN_POINT('Ctrl Pts',(-20.496836459412,21.0692043517748,14.7365837132944));
#134989=CARTESIAN_POINT('Ctrl Pts',(-20.4355917013479,21.1254338132407,
14.7407243559553));
#134990=CARTESIAN_POINT('Ctrl Pts',(-20.3718854170609,21.1784682616447,
14.7448649986162));
#134991=CARTESIAN_POINT('Ctrl Pts',(-20.340529452726,21.2045715933849,14.7469030054635));
#134992=CARTESIAN_POINT('Ctrl Pts',(-20.3085776248467,21.2299015689541,
14.7489410123109));
#134993=CARTESIAN_POINT('Ctrl Pts',(-20.2760730898184,21.2544310817001,
14.7509790191583));
#134994=CARTESIAN_POINT('Ctrl Pts',(-20.2093316088543,21.3047974692387,
14.7551636535513));
#134995=CARTESIAN_POINT('Ctrl Pts',(-20.1399957689001,21.3519843348468,
14.7593482879444));
#134996=CARTESIAN_POINT('Ctrl Pts',(-20.0684012262927,21.3957135664129,
14.7635329223374));
#134997=CARTESIAN_POINT('Ctrl Pts',(-19.9969085896549,21.4393805548305,
14.7677116004214));
#134998=CARTESIAN_POINT('Ctrl Pts',(-19.9231640255691,21.4795994471402,
14.7718902785053));
#134999=CARTESIAN_POINT('Ctrl Pts',(-19.8475347050064,21.5161335017188,
14.7760689565893));
#135000=CARTESIAN_POINT('Ctrl Pts',(-19.7705497832267,21.553322402969,14.7803225344747));
#135001=CARTESIAN_POINT('Ctrl Pts',(-19.6916122567004,21.5866927752846,
14.7845761123602));
#135002=CARTESIAN_POINT('Ctrl Pts',(-19.6111386006649,21.6160421774313,
14.7888296902456));
#135003=CARTESIAN_POINT('Ctrl Pts',(-19.532225083483,21.6448225841468,14.7930008042235));
#135004=CARTESIAN_POINT('Ctrl Pts',(-19.4518349191,21.6697363732163,14.7971719182015));
#135005=CARTESIAN_POINT('Ctrl Pts',(-19.3703822558334,21.6906406240543,
14.8013430321794));
#135006=CARTESIAN_POINT('Ctrl Pts',(-19.2889569247947,21.711537860269,14.8055127464998));
#135007=CARTESIAN_POINT('Ctrl Pts',(-19.2064702481715,21.728428116053,14.8096824608202));
#135008=CARTESIAN_POINT('Ctrl Pts',(-19.1233507011891,21.7412185738555,
14.8138521751405));
#135009=CARTESIAN_POINT('Ctrl Pts',(-19.0402341119568,21.7540085765187,
14.8180217410846));
#135010=CARTESIAN_POINT('Ctrl Pts',(-18.9564851519519,21.7626990021399,
14.8221913070286));
#135011=CARTESIAN_POINT('Ctrl Pts',(-18.8725402767196,21.7672485387236,
14.8263608729727));
#135012=CARTESIAN_POINT('Ctrl Pts',(-18.7856440032315,21.7719580314011,
14.8306770357116));
#135013=CARTESIAN_POINT('Ctrl Pts',(-18.6985383080786,21.7722300013651,
14.8349931984505));
#135014=CARTESIAN_POINT('Ctrl Pts',(-18.6117085473887,21.7680773943348,
14.8393093611894));
#135015=CARTESIAN_POINT('Ctrl Pts',(-18.5277072570202,21.7640600580418,
14.8434849253811));
#135016=CARTESIAN_POINT('Ctrl Pts',(-18.4439646643002,21.7559020718402,
14.8476604895728));
#135017=CARTESIAN_POINT('Ctrl Pts',(-18.3609142114856,21.7436679597627,
14.8518360537645));
#135018=CARTESIAN_POINT('Ctrl Pts',(-18.2736690777334,21.7308159317681,
14.856222515777));
#135019=CARTESIAN_POINT('Ctrl Pts',(-18.187188413865,21.713465300997,14.8606089777895));
#135020=CARTESIAN_POINT('Ctrl Pts',(-18.1019594530762,21.6917508434029,
14.8649954398021));
#135021=CARTESIAN_POINT('Ctrl Pts',(-18.0167304922875,21.6700363858088,
14.8693819018146));
#135022=CARTESIAN_POINT('Ctrl Pts',(-17.932753766134,21.6439583461084,14.8737683638271));
#135023=CARTESIAN_POINT('Ctrl Pts',(-17.8504927560607,21.613709917969,14.8781548258396));
#135024=CARTESIAN_POINT('Ctrl Pts',(-17.7720166970008,21.5848532648472,
14.8823394602327));
#135025=CARTESIAN_POINT('Ctrl Pts',(-17.6948098353987,21.5520941514643,
14.8865240946257));
#135026=CARTESIAN_POINT('Ctrl Pts',(-17.6192877039371,21.5155642748698,
14.8907087290188));
#135027=CARTESIAN_POINT('Ctrl Pts',(-17.543873068882,21.4790863940332,14.8948874071027));
#135028=CARTESIAN_POINT('Ctrl Pts',(-17.4701388113641,21.4388486095631,
14.8990660851867));
#135029=CARTESIAN_POINT('Ctrl Pts',(-17.3984827363062,21.3950315103898,
14.9032447632706));
#135030=CARTESIAN_POINT('Ctrl Pts',(-17.3255422776009,21.3504290212045,
14.907498341156));
#135031=CARTESIAN_POINT('Ctrl Pts',(-17.2547556895192,21.3021178031456,
14.9117519190415));
#135032=CARTESIAN_POINT('Ctrl Pts',(-17.1865186232488,21.2503384683785,
14.9160054969269));
#135033=CARTESIAN_POINT('Ctrl Pts',(-17.1196044656618,21.1995629770549,
14.9201766109048));
#135034=CARTESIAN_POINT('Ctrl Pts',(-17.0551422404864,21.1454529323241,
14.9243477248828));
#135035=CARTESIAN_POINT('Ctrl Pts',(-16.9934762919468,21.0882792071785,
14.9285188388608));
#135036=CARTESIAN_POINT('Ctrl Pts',(-16.9318310360118,21.0311246672285,
14.9326885531811));
#135037=CARTESIAN_POINT('Ctrl Pts',(-16.8729805302658,20.970908801095,14.9368582675015));
#135038=CARTESIAN_POINT('Ctrl Pts',(-16.8172347450929,20.9079416482545,
14.9410279818219));
#135039=CARTESIAN_POINT('Ctrl Pts',(-16.7614909435942,20.8449767360556,
14.9451975477659));
#135040=CARTESIAN_POINT('Ctrl Pts',(-16.7088519473105,20.7792610768136,
14.9493671137099));
#135041=CARTESIAN_POINT('Ctrl Pts',(-16.6595887382006,20.7111392991718,
14.953536679654));
#135042=CARTESIAN_POINT('Ctrl Pts',(-16.608593495431,20.6406224438653,14.9578528423929));
#135043=CARTESIAN_POINT('Ctrl Pts',(-16.5612161510352,20.5675275511998,
14.9621690051318));
#135044=CARTESIAN_POINT('Ctrl Pts',(-16.5177085337784,20.4922697361419,
14.9664851678708));
#135045=CARTESIAN_POINT('Ctrl Pts',(-16.4756181725776,20.4194634364939,
14.9706607320624));
#135046=CARTESIAN_POINT('Ctrl Pts',(-16.4371494708084,20.3446334053666,
14.9748362962541));
#135047=CARTESIAN_POINT('Ctrl Pts',(-16.4024827880432,20.2681790247396,
14.9790118604458));
#135048=CARTESIAN_POINT('Ctrl Pts',(-16.3660651735437,20.1878631150998,
14.9833983224583));
#135049=CARTESIAN_POINT('Ctrl Pts',(-16.3338439651087,20.1057549952923,
14.9877847844709));
#135050=CARTESIAN_POINT('Ctrl Pts',(-16.3059695675779,20.0223373029956,
14.9921712464834));
#135051=CARTESIAN_POINT('Ctrl Pts',(-16.2780951700472,19.9389196106989,
14.996557708496));
#135052=CARTESIAN_POINT('Ctrl Pts',(-16.2545676653735,19.8541929253278,
15.0009441705085));
#135053=CARTESIAN_POINT('Ctrl Pts',(-16.2354754819719,19.7686515334978,
15.0053306325211));
#135054=CARTESIAN_POINT('Ctrl Pts',(-16.2172617582301,19.6870460279088,
15.0095152669141));
#135055=CARTESIAN_POINT('Ctrl Pts',(-16.2030163785017,19.6043953888036,
15.0136999013072));
#135056=CARTESIAN_POINT('Ctrl Pts',(-16.1928535263698,19.5211202985239,
15.0178845357002));
#135057=CARTESIAN_POINT('Ctrl Pts',(-16.1827051397999,19.4379637400279,
15.0220632137842));
#135058=CARTESIAN_POINT('Ctrl Pts',(-16.1766277936582,19.3541849485907,
15.0262418918681));
#135059=CARTESIAN_POINT('Ctrl Pts',(-16.1746849654928,19.270216164561,15.0304205699521));
#135060=CARTESIAN_POINT('Ctrl Pts',(-16.1727073135288,19.1847423004249,
15.0346741478375));
#135061=CARTESIAN_POINT('Ctrl Pts',(-16.1750139649457,19.0990720360281,
15.0389277257229));
#135062=CARTESIAN_POINT('Ctrl Pts',(-16.1816167614736,19.0136682902079,
15.0431813036084));
#135063=CARTESIAN_POINT('Ctrl Pts',(-16.1880915499066,18.9299202626522,
15.0473524175863));
#135064=CARTESIAN_POINT('Ctrl Pts',(-16.1986973545604,18.8464289917134,
15.0515235315643));
#135065=CARTESIAN_POINT('Ctrl Pts',(-16.2133928011124,18.7636306348037,
15.0556946455422));
#135066=CARTESIAN_POINT('Ctrl Pts',(-16.2280833164655,18.6808600616822,
15.0598643598626));
#135067=CARTESIAN_POINT('Ctrl Pts',(-16.2468606679443,18.5987823933903,
15.064034074183));
#135068=CARTESIAN_POINT('Ctrl Pts',(-16.2696319425036,18.5178260844556,
15.0682037885034));
#135069=CARTESIAN_POINT('Ctrl Pts',(-16.2924024067631,18.4368726562939,
15.0723733544474));
#135070=CARTESIAN_POINT('Ctrl Pts',(-16.3191663861463,18.3570409507694,
15.0765429203914));
#135071=CARTESIAN_POINT('Ctrl Pts',(-16.3497807798975,18.278745361774,15.0807124863355));
#135072=CARTESIAN_POINT('Ctrl Pts',(-16.3814715379661,18.1976969964576,
15.0850286490744));
#135073=CARTESIAN_POINT('Ctrl Pts',(-16.4172883172411,18.1182952684027,
15.0893448118133));
#135074=CARTESIAN_POINT('Ctrl Pts',(-16.4570183818635,18.0409766196061,
15.0936609745522));
#135075=CARTESIAN_POINT('Ctrl Pts',(-16.4954542438097,17.9661766176615,
15.0978365387439));
#135076=CARTESIAN_POINT('Ctrl Pts',(-16.5375520792275,17.8933264506922,
15.1020121029356));
#135077=CARTESIAN_POINT('Ctrl Pts',(-16.5830736962918,17.8227939504468,
15.1061876671273));
#135078=CARTESIAN_POINT('Ctrl Pts',(-16.6308945020166,17.7486990212891,
15.1105741291398));
#135079=CARTESIAN_POINT('Ctrl Pts',(-16.6824937078806,17.677162516164,15.1149605911524));
#135080=CARTESIAN_POINT('Ctrl Pts',(-16.7375469032623,17.6085721443614,
15.1193470531649));
#135081=CARTESIAN_POINT('Ctrl Pts',(-16.7926000986441,17.5399817725587,
15.1237335151774));
#135082=CARTESIAN_POINT('Ctrl Pts',(-16.851106840707,17.474337916614,15.12811997719));
#135083=CARTESIAN_POINT('Ctrl Pts',(-16.9126993772537,17.4119824788001,
15.1325064392025));
#135084=CARTESIAN_POINT('Ctrl Pts',(-16.9714542743061,17.3524998282257,
15.1366908118298));
#135085=CARTESIAN_POINT('Ctrl Pts',(-17.0332355735151,17.295787869,15.1408751844571));
#135086=CARTESIAN_POINT('Ctrl Pts',(-17.0977514090542,17.2421702591062,
15.1450595570844));
#135087=CARTESIAN_POINT('Ctrl Pts',(-17.1229131590333,17.2212589141108,
15.1466914996452));
#135088=CARTESIAN_POINT('Ctrl Pts',(-17.1484904128431,17.2008178921216,
15.1483234422061));
#135089=CARTESIAN_POINT('Ctrl Pts',(-17.174464231106,17.180864983421,15.149955384767));
#135090=CARTESIAN_POINT('Ctrl Pts',(-17.1732300624786,17.1792869614928,
14.3497865218036));
#135091=CARTESIAN_POINT('Ctrl Pts',(-17.2767521095298,17.0982003735101,
14.3563415475737));
#135092=CARTESIAN_POINT('Ctrl Pts',(-18.0960849484291,16.5548825890784,
14.4052885089043));
#135093=CARTESIAN_POINT('Ctrl Pts',(-20.1784867160069,16.5507838647211,
14.4966274057954));
#135094=CARTESIAN_POINT('Ctrl Pts',(-21.2671018326456,18.2345793421635,
14.5845735760146));
#135095=CARTESIAN_POINT('Ctrl Pts',(-21.2979709281649,19.1465375840163,
14.6301278106733));
#135096=CARTESIAN_POINT('Ctrl Pts',(-21.2976211493107,19.2098682725933,
14.6332901097715));
#135097=CARTESIAN_POINT('',(-21.2936354898062,19.2115601738724,14.5667099150531));
#135098=CARTESIAN_POINT('Ctrl Pts',(-17.1756294966411,17.1824128461128,
14.2834124313123));
#135099=CARTESIAN_POINT('Ctrl Pts',(-17.6442977536355,16.8288108709757,
14.3125636725423));
#135100=CARTESIAN_POINT('Ctrl Pts',(-19.0929372054435,16.3386618105897,
14.3841068493327));
#135101=CARTESIAN_POINT('Ctrl Pts',(-20.9482576099774,17.4308694729993,
14.4785393356381));
#135102=CARTESIAN_POINT('Ctrl Pts',(-21.2889976010488,18.7496082874005,
14.5438205807135));
#135103=CARTESIAN_POINT('Ctrl Pts',(-21.2898971100035,19.211558854651,14.5667098902285));
#135104=CARTESIAN_POINT('Ctrl Pts',(-21.2939999386838,19.2115603024813,
14.5667099174733));
#135105=CARTESIAN_POINT('Ctrl Pts',(-21.2939802627011,19.301459091566,14.5711571992722));
#135106=CARTESIAN_POINT('Ctrl Pts',(-21.2892209204019,19.3912344818061,
14.5756044810712));
#135107=CARTESIAN_POINT('Ctrl Pts',(-21.2797861099485,19.4803939167712,
14.5800517628701));
#135108=CARTESIAN_POINT('Ctrl Pts',(-21.270316767046,19.5698796851229,14.584515322212));
#135109=CARTESIAN_POINT('Ctrl Pts',(-21.2561377674645,19.6587446305213,
14.5889788815539));
#135110=CARTESIAN_POINT('Ctrl Pts',(-21.2373647797492,19.7465042292186,
14.5934424408958));
#135111=CARTESIAN_POINT('Ctrl Pts',(-21.2185553401057,19.8344342326829,
14.5979146672303));
#135112=CARTESIAN_POINT('Ctrl Pts',(-21.1951342035234,19.9212542602487,
14.6023868935647));
#135113=CARTESIAN_POINT('Ctrl Pts',(-21.1672666877215,20.0064955854214,
14.6068591198992));
#135114=CARTESIAN_POINT('Ctrl Pts',(-21.1393161596827,20.0919908289243,
14.6113446681786));
#135115=CARTESIAN_POINT('Ctrl Pts',(-21.1068928974848,20.1758976314735,
14.615830216458));
#135116=CARTESIAN_POINT('Ctrl Pts',(-21.0702104967872,20.2577666954491,
14.6203157647375));
#135117=CARTESIAN_POINT('Ctrl Pts',(-21.0568477853949,20.2875900617789,
14.6219497659466));
#135118=CARTESIAN_POINT('Ctrl Pts',(-21.0429203172376,20.3171432681498,
14.6235837671558));
#135119=CARTESIAN_POINT('Ctrl Pts',(-21.0284398795323,20.3464054955,14.6252177683649));
#135120=CARTESIAN_POINT('Ctrl Pts',(-20.9913558570061,20.4213452949944,
14.6294024027579));
#135121=CARTESIAN_POINT('Ctrl Pts',(-20.9505274948145,20.4946058152548,
14.633587037151));
#135122=CARTESIAN_POINT('Ctrl Pts',(-20.9061301751472,20.5657879916116,
14.637771671544));
#135123=CARTESIAN_POINT('Ctrl Pts',(-20.8617960495691,20.636868848951,14.641950349628));
#135124=CARTESIAN_POINT('Ctrl Pts',(-20.8139032983065,20.7058768514385,
14.6461290277119));
#135125=CARTESIAN_POINT('Ctrl Pts',(-20.7626740190628,20.7724357893874,
14.6503077057959));
#135126=CARTESIAN_POINT('Ctrl Pts',(-20.7105264918065,20.8401877484639,
14.6545612836813));
#135127=CARTESIAN_POINT('Ctrl Pts',(-20.6549218593555,20.9054015483268,
14.6588148615668));
#135128=CARTESIAN_POINT('Ctrl Pts',(-20.5961416680528,20.9677095400496,
14.6630684394522));
#135129=CARTESIAN_POINT('Ctrl Pts',(-20.5385010454587,21.0288095697688,
14.6672395534301));
#135130=CARTESIAN_POINT('Ctrl Pts',(-20.4778072242622,21.0871151053885,
14.6714106674081));
#135131=CARTESIAN_POINT('Ctrl Pts',(-20.4143663508875,21.1423127470208,
14.6755817813861));
#135132=CARTESIAN_POINT('Ctrl Pts',(-20.3509467657105,21.1974918665513,
14.6797514957064));
#135133=CARTESIAN_POINT('Ctrl Pts',(-20.2847823058331,21.2495648615671,
14.6839212100268));
#135134=CARTESIAN_POINT('Ctrl Pts',(-20.2162143833073,21.2982566976577,
14.6880909243472));
#135135=CARTESIAN_POINT('Ctrl Pts',(-20.1476489007224,21.3469468010838,
14.6922604902912));
#135136=CARTESIAN_POINT('Ctrl Pts',(-20.0766805011099,21.3922557191444,
14.6964300562353));
#135137=CARTESIAN_POINT('Ctrl Pts',(-20.0036808175629,21.433950881489,14.7005996221793));
#135138=CARTESIAN_POINT('Ctrl Pts',(-19.9281145551974,21.477111994305,14.7049157849182));
#135139=CARTESIAN_POINT('Ctrl Pts',(-19.850371969323,21.5164002423867,14.7092319476572));
#135140=CARTESIAN_POINT('Ctrl Pts',(-19.7708927266886,21.5516096371117,
14.7135481103961));
#135141=CARTESIAN_POINT('Ctrl Pts',(-19.6940025120233,21.5856720895069,
14.7177236745878));
#135142=CARTESIAN_POINT('Ctrl Pts',(-19.6154875027973,21.6159172197028,
14.7218992387794));
#135143=CARTESIAN_POINT('Ctrl Pts',(-19.5357640795052,21.6422084157503,
14.7260748029711));
#135144=CARTESIAN_POINT('Ctrl Pts',(-19.4520140156271,21.6698275176088,
14.7304612649837));
#135145=CARTESIAN_POINT('Ctrl Pts',(-19.3669308187544,21.6930826078309,
14.7348477269962));
#135146=CARTESIAN_POINT('Ctrl Pts',(-19.2810104439706,21.7118757614458,
14.7392341890088));
#135147=CARTESIAN_POINT('Ctrl Pts',(-19.1950900691869,21.7306689150607,
14.7436206510213));
#135148=CARTESIAN_POINT('Ctrl Pts',(-19.1083331013483,21.7450001125529,
14.7480071130338));
#135149=CARTESIAN_POINT('Ctrl Pts',(-19.021240449396,21.7548342957494,14.7523935750464));
#135150=CARTESIAN_POINT('Ctrl Pts',(-18.9381550594623,21.7642159935992,
14.7565782094394));
#135151=CARTESIAN_POINT('Ctrl Pts',(-18.8544549375686,21.7695403323457,
14.7607628438325));
#135152=CARTESIAN_POINT('Ctrl Pts',(-18.770570565002,21.7707387745189,14.7649474782255));
#135153=CARTESIAN_POINT('Ctrl Pts',(-18.6868055914569,21.7719355108579,
14.7691261563095));
#135154=CARTESIAN_POINT('Ctrl Pts',(-18.6028573442174,21.7690180091444,
14.7733048343934));
#135155=CARTESIAN_POINT('Ctrl Pts',(-18.5191623733682,21.7619693832312,
14.7774835124774));
#135156=CARTESIAN_POINT('Ctrl Pts',(-18.4339672303171,21.7547944157644,
14.7817370903628));
#135157=CARTESIAN_POINT('Ctrl Pts',(-18.3490350120195,21.7433387124852,
14.7859906682482));
#135158=CARTESIAN_POINT('Ctrl Pts',(-18.2648272487365,21.7276400079216,
14.7902442461337));
#135159=CARTESIAN_POINT('Ctrl Pts',(-18.1822520172626,21.7122456533795,
14.7944153601116));
#135160=CARTESIAN_POINT('Ctrl Pts',(-18.1003738745931,21.6927714353377,
14.7985864740896));
#135161=CARTESIAN_POINT('Ctrl Pts',(-18.0196220516901,21.6693051370748,
14.8027575880676));
#135162=CARTESIAN_POINT('Ctrl Pts',(-17.9388973258412,21.645846713155,14.8069273023879));
#135163=CARTESIAN_POINT('Ctrl Pts',(-17.8592986105396,21.6183989977105,
14.8110970167083));
#135164=CARTESIAN_POINT('Ctrl Pts',(-17.7812419660678,21.5871001933373,
14.8152667310287));
#135165=CARTESIAN_POINT('Ctrl Pts',(-17.7031880991865,21.5558025027099,
14.8194362969727));
#135166=CARTESIAN_POINT('Ctrl Pts',(-17.6266766207012,21.5206541676232,
14.8236058629168));
#135167=CARTESIAN_POINT('Ctrl Pts',(-17.5521042434164,21.4818417867764,
14.8277754288608));
#135168=CARTESIAN_POINT('Ctrl Pts',(-17.4749099933414,21.4416648104993,
14.8320915915997));
#135169=CARTESIAN_POINT('Ctrl Pts',(-17.3997942069759,21.3975615823359,
14.8364077543386));
#135170=CARTESIAN_POINT('Ctrl Pts',(-17.3271680714248,21.349790294709,14.8407239170776));
#135171=CARTESIAN_POINT('Ctrl Pts',(-17.2569077246003,21.3035751517518,
14.8448994812692));
#135172=CARTESIAN_POINT('Ctrl Pts',(-17.188977671162,21.253927569593,14.8490750454609));
#135173=CARTESIAN_POINT('Ctrl Pts',(-17.1237181590043,21.2011237128781,
14.8532506096526));
#135174=CARTESIAN_POINT('Ctrl Pts',(-17.0551625440275,21.1456528588898,
14.8576370716651));
#135175=CARTESIAN_POINT('Ctrl Pts',(-16.9895547726119,21.0866988942974,
14.8620235336777));
#135176=CARTESIAN_POINT('Ctrl Pts',(-16.9272456352412,21.0246258339098,
14.8664099956902));
#135177=CARTESIAN_POINT('Ctrl Pts',(-16.8649364978706,20.9625527735222,
14.8707964577027));
#135178=CARTESIAN_POINT('Ctrl Pts',(-16.8059263275258,20.8973610985477,
14.8751829197153));
#135179=CARTESIAN_POINT('Ctrl Pts',(-16.7505157350919,20.8294530178111,
14.8795693817278));
#135180=CARTESIAN_POINT('Ctrl Pts',(-16.697654666154,20.764669488533,14.8837540161209));
#135181=CARTESIAN_POINT('Ctrl Pts',(-16.6478724513804,20.6971728954314,
14.8879386505139));
#135182=CARTESIAN_POINT('Ctrl Pts',(-16.6014597312931,20.6272881071108,
14.892123284907));
#135183=CARTESIAN_POINT('Ctrl Pts',(-16.5551130739681,20.5575027911364,
14.8963019629909));
#135184=CARTESIAN_POINT('Ctrl Pts',(-16.5121266371783,20.4853364119635,
14.9004806410748));
#135185=CARTESIAN_POINT('Ctrl Pts',(-16.4727509157821,20.4111468989768,
14.9046593191588));
#135186=CARTESIAN_POINT('Ctrl Pts',(-16.4326694128786,20.3356275922887,
14.9089128970442));
#135187=CARTESIAN_POINT('Ctrl Pts',(-16.3963296475344,20.2580122826049,
14.9131664749297));
#135188=CARTESIAN_POINT('Ctrl Pts',(-16.3639497085599,20.1787094688205,
14.9174200528151));
#135189=CARTESIAN_POINT('Ctrl Pts',(-16.3321975178868,20.1009440948281,
14.9215911667931));
#135190=CARTESIAN_POINT('Ctrl Pts',(-16.3042531677129,20.0215565094719,
14.925762280771));
#135191=CARTESIAN_POINT('Ctrl Pts',(-16.2802751807719,19.9409551434874,
14.929933394749));
#135192=CARTESIAN_POINT('Ctrl Pts',(-16.2563052398759,19.8603808240697,
14.9341031090693));
#135193=CARTESIAN_POINT('Ctrl Pts',(-16.2362991499858,19.7785939734879,
14.9382728233897));
#135194=CARTESIAN_POINT('Ctrl Pts',(-16.2203659101292,19.6960192390406,
14.9424425377101));
#135195=CARTESIAN_POINT('Ctrl Pts',(-16.2044332372457,19.6134474429567,
14.9466121036541));
#135196=CARTESIAN_POINT('Ctrl Pts',(-16.1925732125599,19.530088270613,14.9507816695982));
#135197=CARTESIAN_POINT('Ctrl Pts',(-16.1848436692124,19.4463762970338,
14.9549512355422));
#135198=CARTESIAN_POINT('Ctrl Pts',(-16.1768423646562,19.3597211137334,
14.9592673982811));
#135199=CARTESIAN_POINT('Ctrl Pts',(-16.1732674495782,19.2726883838098,
14.9635835610201));
#135200=CARTESIAN_POINT('Ctrl Pts',(-16.1741243927921,19.185763605208,14.967899723759));
#135201=CARTESIAN_POINT('Ctrl Pts',(-16.174953421171,19.1016703921263,14.9720752879507));
#135202=CARTESIAN_POINT('Ctrl Pts',(-16.1799299313355,19.0176786727672,
14.9762508521424));
#135203=CARTESIAN_POINT('Ctrl Pts',(-16.1890058822548,18.9342240244489,
14.980426416334));
#135204=CARTESIAN_POINT('Ctrl Pts',(-16.198540237879,18.8465542802385,14.9848128783466));
#135205=CARTESIAN_POINT('Ctrl Pts',(-16.2125989501167,18.7594778642492,
14.9891993403591));
#135206=CARTESIAN_POINT('Ctrl Pts',(-16.2310658163554,18.6734867700759,
14.9935858023717));
#135207=CARTESIAN_POINT('Ctrl Pts',(-16.2495326825942,18.5874956759026,
14.9979722643842));
#135208=CARTESIAN_POINT('Ctrl Pts',(-16.2724074784504,18.5025904439986,
15.0023587263968));
#135209=CARTESIAN_POINT('Ctrl Pts',(-16.2995147249237,18.4192415485537,
15.0067451884093));
#135210=CARTESIAN_POINT('Ctrl Pts',(-16.3253715040259,18.3397375686843,
15.0109293012963));
#135211=CARTESIAN_POINT('Ctrl Pts',(-16.3551750808439,18.2613536084849,
15.0151134141832));
#135212=CARTESIAN_POINT('Ctrl Pts',(-16.3888096569691,18.1845097394741,
15.0192975270702));
#135213=CARTESIAN_POINT('Ctrl Pts',(-16.4223989481496,18.1077693315666,
15.0234760065482));
#135214=CARTESIAN_POINT('Ctrl Pts',(-16.4598088142964,18.0325653152782,
15.0276544860263));
#135215=CARTESIAN_POINT('Ctrl Pts',(-16.5008739124279,17.9593020024763,
15.0318329655043));
#135216=CARTESIAN_POINT('Ctrl Pts',(-16.5429986601539,17.884148192799,15.0361192670572));
#135217=CARTESIAN_POINT('Ctrl Pts',(-16.5889697495617,17.8110370999845,
15.0404055686101));
#135218=CARTESIAN_POINT('Ctrl Pts',(-16.6385563150878,17.7403825231007,
15.0446918701631));
#135219=CARTESIAN_POINT('Ctrl Pts',(-16.686808182088,17.6716297226077,15.0488627993302));
#135220=CARTESIAN_POINT('Ctrl Pts',(-16.7384830670581,17.6052032663847,
15.0530337284974));
#135221=CARTESIAN_POINT('Ctrl Pts',(-16.7933230566453,17.5414572477676,
15.0572046576646));
#135222=CARTESIAN_POINT('Ctrl Pts',(-16.8504384458537,17.4750663040202,
15.0615486454104));
#135223=CARTESIAN_POINT('Ctrl Pts',(-16.9109870226805,17.4115835115971,
15.0658926331562));
#135224=CARTESIAN_POINT('Ctrl Pts',(-16.9746305398746,17.35137124598,15.0702366209019));
#135225=CARTESIAN_POINT('Ctrl Pts',(-17.0382740570687,17.2911589803629,
15.0745806086477));
#135226=CARTESIAN_POINT('Ctrl Pts',(-17.1050121046529,17.2342176296957,
15.0789245963935));
#135227=CARTESIAN_POINT('Ctrl Pts',(-17.174464231106,17.180864983421,15.0832685841393));
#135228=CARTESIAN_POINT('Origin',(-18.734,19.211,-1.76670989022852));
#135229=CARTESIAN_POINT('',(-17.174464231106,17.180864983421,15.9499155238083));
#135230=CARTESIAN_POINT('',(-17.172599350298,17.1784745189047,15.8832287057516));
#135231=CARTESIAN_POINT('',(-17.174464231106,17.180864983421,-1.76670989022852));
#135232=CARTESIAN_POINT('',(-21.293999428374,19.2092892327452,15.4332901097416));
#135233=CARTESIAN_POINT('Ctrl Pts',(-21.2939994283744,19.2092892333484,
15.4332901097715));
#135234=CARTESIAN_POINT('Ctrl Pts',(-21.2940559692553,19.2938972788889,
15.437482057942));
#135235=CARTESIAN_POINT('Ctrl Pts',(-21.2899137324165,19.3785303101354,
15.4416740061124));
#135236=CARTESIAN_POINT('Ctrl Pts',(-21.2815918669692,19.4627452667924,
15.4458659542829));
#135237=CARTESIAN_POINT('Ctrl Pts',(-21.2732695913204,19.546964374574,15.4500581090829));
#135238=CARTESIAN_POINT('Ctrl Pts',(-21.2607673227297,19.6307649161162,
15.4542502638829));
#135239=CARTESIAN_POINT('Ctrl Pts',(-21.2441560631152,19.7137091990464,
15.4584424186829));
#135240=CARTESIAN_POINT('Ctrl Pts',(-21.2275392030058,19.7966814466854,
15.4626359868702));
#135241=CARTESIAN_POINT('Ctrl Pts',(-21.2068106889623,19.878796418332,15.4668295550574));
#135242=CARTESIAN_POINT('Ctrl Pts',(-21.1820923104738,19.9596281048684,
15.4710231232446));
#135243=CARTESIAN_POINT('Ctrl Pts',(-21.157341575289,20.0405656011908,15.4752221808701));
#135244=CARTESIAN_POINT('Ctrl Pts',(-21.1285906849039,20.1202160261787,
15.4794212384956));
#135245=CARTESIAN_POINT('Ctrl Pts',(-21.0960107310932,20.1981703531815,
15.483620296121));
#135246=CARTESIAN_POINT('Ctrl Pts',(-21.0634063961448,20.2761830171356,
15.4878224961022));
#135247=CARTESIAN_POINT('Ctrl Pts',(-21.0269674888695,20.3524966484648,
15.4920246960833));
#135248=CARTESIAN_POINT('Ctrl Pts',(-20.9869114421225,20.4267261344371,
15.4962268960644));
#135249=CARTESIAN_POINT('Ctrl Pts',(-20.9467843119665,20.5010873479597,
15.5004365532642));
#135250=CARTESIAN_POINT('Ctrl Pts',(-20.903027463882,20.5733566470828,15.504646210464));
#135251=CARTESIAN_POINT('Ctrl Pts',(-20.8559018807143,20.6431775059751,
15.5088558676638));
#135252=CARTESIAN_POINT('Ctrl Pts',(-20.8365799691026,20.6718046841124,
15.5105818648582));
#135253=CARTESIAN_POINT('Ctrl Pts',(-20.8166922183619,20.7000206489315,
15.5123078620525));
#135254=CARTESIAN_POINT('Ctrl Pts',(-20.7962584977301,20.7278025212729,
15.5140338592469));
#135255=CARTESIAN_POINT('Ctrl Pts',(-20.7467174843304,20.7951589334867,
15.5182184936399));
#135256=CARTESIAN_POINT('Ctrl Pts',(-20.6937808669813,20.8602110167103,
15.522403128033));
#135257=CARTESIAN_POINT('Ctrl Pts',(-20.6376906991395,20.9225962497066,
15.526587762426));
#135258=CARTESIAN_POINT('Ctrl Pts',(-20.5816803687091,20.9848926850455,
15.53076644051));
#135259=CARTESIAN_POINT('Ctrl Pts',(-20.5225257086781,21.0445294709031,
15.5349451185939));
#135260=CARTESIAN_POINT('Ctrl Pts',(-20.4605108062945,21.1011747103769,
15.5391237966779));
#135261=CARTESIAN_POINT('Ctrl Pts',(-20.3973843313549,21.1588352750581,
15.5433773745633));
#135262=CARTESIAN_POINT('Ctrl Pts',(-20.3312943514667,21.213395603145,15.5476309524487));
#135263=CARTESIAN_POINT('Ctrl Pts',(-20.2625820107878,21.2645425577026,
15.5518845303342));
#135264=CARTESIAN_POINT('Ctrl Pts',(-20.195201792914,21.3146979287411,15.5560556443121));
#135265=CARTESIAN_POINT('Ctrl Pts',(-20.1253003720614,21.3615708076597,
15.5602267582901));
#135266=CARTESIAN_POINT('Ctrl Pts',(-20.0532336923064,21.4049057557433,
15.564397872268));
#135267=CARTESIAN_POINT('Ctrl Pts',(-19.9811911952217,21.4482261623666,
15.5685675865884));
#135268=CARTESIAN_POINT('Ctrl Pts',(-19.9069852761388,21.4880107590574,
15.5727373009088));
#135269=CARTESIAN_POINT('Ctrl Pts',(-19.8309999421956,21.5240480165407,
15.5769070152291));
#135270=CARTESIAN_POINT('Ctrl Pts',(-19.7550173121366,21.5600839916638,
15.5810765811732));
#135271=CARTESIAN_POINT('Ctrl Pts',(-19.677255809133,21.592372696345,15.5852461471172));
#135272=CARTESIAN_POINT('Ctrl Pts',(-19.5981218233861,21.6207496704736,
15.5894157130613));
#135273=CARTESIAN_POINT('Ctrl Pts',(-19.5162055843226,21.6501243440058,
15.5937318758002));
#135274=CARTESIAN_POINT('Ctrl Pts',(-19.4328190502825,21.6753069180703,
15.5980480385391));
#135275=CARTESIAN_POINT('Ctrl Pts',(-19.3484309915966,21.696170931056,15.602364201278));
#135276=CARTESIAN_POINT('Ctrl Pts',(-19.2667918650464,21.7163553010132,
15.6065397654697));
#135277=CARTESIAN_POINT('Ctrl Pts',(-19.1842159325099,21.7324980994094,
15.6107153296614));
#135278=CARTESIAN_POINT('Ctrl Pts',(-19.1011369778114,21.7445371399534,
15.6148908938531));
#135279=CARTESIAN_POINT('Ctrl Pts',(-19.0138619026126,21.7571842438153,
15.6192773558656));
#135280=CARTESIAN_POINT('Ctrl Pts',(-18.9260322359069,21.7653020795901,
15.6236638178782));
#135281=CARTESIAN_POINT('Ctrl Pts',(-18.8381534037013,21.7688803858854,
15.6280502798907));
#135282=CARTESIAN_POINT('Ctrl Pts',(-18.7502745714957,21.7724586921808,
15.6324367419032));
#135283=CARTESIAN_POINT('Ctrl Pts',(-18.6623471531412,21.771497551399,15.6368232039158));
#135284=CARTESIAN_POINT('Ctrl Pts',(-18.5748705298081,21.7660494734381,
15.6412096659283));
#135285=CARTESIAN_POINT('Ctrl Pts',(-18.4914188355861,21.7608520696202,
15.6453943003213));
#135286=CARTESIAN_POINT('Ctrl Pts',(-18.4080667413617,21.7515522106695,
15.6495789347144));
#135287=CARTESIAN_POINT('Ctrl Pts',(-18.3252500890704,21.7381571993675,
15.6537635691074));
#135288=CARTESIAN_POINT('Ctrl Pts',(-18.2425513160331,21.7247812542061,
15.6579422471914));
#135289=CARTESIAN_POINT('Ctrl Pts',(-18.1603869213351,21.7073218076316,
15.6621209252753));
#135290=CARTESIAN_POINT('Ctrl Pts',(-18.0791897487866,21.6858380825634,
15.6662996033592));
#135291=CARTESIAN_POINT('Ctrl Pts',(-17.9965371752754,21.6639692771633,
15.6705531812447));
#135292=CARTESIAN_POINT('Ctrl Pts',(-17.9148873210955,21.6379305338184,
15.6748067591301));
#135293=CARTESIAN_POINT('Ctrl Pts',(-17.8346881397166,21.6078392056943,
15.6790603370156));
#135294=CARTESIAN_POINT('Ctrl Pts',(-17.7560437759646,21.5783312566844,
15.6832314509935));
#135295=CARTESIAN_POINT('Ctrl Pts',(-17.6787947892658,21.5449266242313,
15.6874025649715));
#135296=CARTESIAN_POINT('Ctrl Pts',(-17.6033486289331,21.5077863368421,
15.6915736789494));
#135297=CARTESIAN_POINT('Ctrl Pts',(-17.5279277852881,21.470658512235,15.6957433932698));
#135298=CARTESIAN_POINT('Ctrl Pts',(-17.4543089789471,21.4297977252417,
15.6999131075901));
#135299=CARTESIAN_POINT('Ctrl Pts',(-17.3828779283357,21.3854123683104,
15.7040828219105));
#135300=CARTESIAN_POINT('Ctrl Pts',(-17.3114494195476,21.3410285908007,
15.7082523878546));
#135301=CARTESIAN_POINT('Ctrl Pts',(-17.2422089019967,21.2931207362396,
15.7124219537986));
#135302=CARTESIAN_POINT('Ctrl Pts',(-17.1755146319181,21.2419414953352,
15.7165915197426));
#135303=CARTESIAN_POINT('Ctrl Pts',(-17.1064754735796,21.1889628554569,
15.7209076824816));
#135304=CARTESIAN_POINT('Ctrl Pts',(-17.0401653646947,21.13247882625,15.7252238452205));
#135305=CARTESIAN_POINT('Ctrl Pts',(-16.9769443759548,21.0728151181068,
15.7295400079594));
#135306=CARTESIAN_POINT('Ctrl Pts',(-16.9157828042734,21.0150949489809,
15.7337155721511));
#135307=CARTESIAN_POINT('Ctrl Pts',(-16.8575124793698,20.9543994482419,
15.7378911363428));
#135308=CARTESIAN_POINT('Ctrl Pts',(-16.8024204890304,20.8910596991781,
15.7420667005344));
#135309=CARTESIAN_POINT('Ctrl Pts',(-16.7445459332276,20.8245208099649,
15.746453162547));
#135310=CARTESIAN_POINT('Ctrl Pts',(-16.6901795852498,20.7550639901493,
15.7508396245595));
#135311=CARTESIAN_POINT('Ctrl Pts',(-16.6396036508155,20.6831086687207,
15.7552260865721));
#135312=CARTESIAN_POINT('Ctrl Pts',(-16.5890277163812,20.611153347292,15.7596125485846));
#135313=CARTESIAN_POINT('Ctrl Pts',(-16.5422424397948,20.5367000559955,
15.7639990105972));
#135314=CARTESIAN_POINT('Ctrl Pts',(-16.499473974098,20.4601971179787,15.7683854726097));
#135315=CARTESIAN_POINT('Ctrl Pts',(-16.458673348906,20.3872141935448,15.7725701070028));
#135316=CARTESIAN_POINT('Ctrl Pts',(-16.4213761508428,20.3120944357928,
15.7767547413958));
#135317=CARTESIAN_POINT('Ctrl Pts',(-16.3878121523981,20.2352082716739,
15.7809393757889));
#135318=CARTESIAN_POINT('Ctrl Pts',(-16.3542959281508,20.158431545493,15.7851180538728));
#135319=CARTESIAN_POINT('Ctrl Pts',(-16.3245025312236,20.0798938250632,
15.7892967319567));
#135320=CARTESIAN_POINT('Ctrl Pts',(-16.2986164546586,19.9999911197726,
15.7934754100407));
#135321=CARTESIAN_POINT('Ctrl Pts',(-16.272266388775,19.9186562159147,15.7977289879261));
#135322=CARTESIAN_POINT('Ctrl Pts',(-16.249965333752,19.8359073320103,15.8019825658115));
#135323=CARTESIAN_POINT('Ctrl Pts',(-16.2318570828658,19.75218464708,15.806236143697));
#135324=CARTESIAN_POINT('Ctrl Pts',(-16.2140998957584,19.6700850897684,
15.8104072576749));
#135325=CARTESIAN_POINT('Ctrl Pts',(-16.2003744938966,19.587049622894,15.8145783716529));
#135326=CARTESIAN_POINT('Ctrl Pts',(-16.1907660223746,19.5035080085253,
15.8187494856308));
#135327=CARTESIAN_POINT('Ctrl Pts',(-16.1811607750679,19.4199944273522,
15.8229191999512));
#135328=CARTESIAN_POINT('Ctrl Pts',(-16.1756697669882,19.3359754926348,
15.8270889142716));
#135329=CARTESIAN_POINT('Ctrl Pts',(-16.1743265551335,19.2518883314074,
15.8312586285919));
#135330=CARTESIAN_POINT('Ctrl Pts',(-16.172983391076,19.1678041623621,15.835428194536));
#135331=CARTESIAN_POINT('Ctrl Pts',(-16.1757877362795,19.0836522316217,
15.83959776048));
#135332=CARTESIAN_POINT('Ctrl Pts',(-16.182721035153,18.9998705526721,15.8437673264241));
#135333=CARTESIAN_POINT('Ctrl Pts',(-16.1898981002617,18.9131432132465,
15.848083489163));
#135334=CARTESIAN_POINT('Ctrl Pts',(-16.2014998257646,18.8268131717714,
15.8523996519019));
#135335=CARTESIAN_POINT('Ctrl Pts',(-16.2174472402024,18.7413594915735,
15.8567158146408));
#135336=CARTESIAN_POINT('Ctrl Pts',(-16.2328751692923,18.6586894560197,
15.8608913788325));
#135337=CARTESIAN_POINT('Ctrl Pts',(-16.2523698584564,18.5768400108858,
15.8650669430242));
#135338=CARTESIAN_POINT('Ctrl Pts',(-16.275808314218,18.4962317606719,15.8692425072159));
#135339=CARTESIAN_POINT('Ctrl Pts',(-16.3004305906604,18.4115521793678,
15.8736289692284));
#135340=CARTESIAN_POINT('Ctrl Pts',(-16.3294053113241,18.3282430251664,
15.8780154312409));
#135341=CARTESIAN_POINT('Ctrl Pts',(-16.3625325554082,18.2467686173739,
15.8824018932535));
#135342=CARTESIAN_POINT('Ctrl Pts',(-16.3956597994922,18.1652942095814,
15.886788355266));
#135343=CARTESIAN_POINT('Ctrl Pts',(-16.4329392521203,18.0856550414426,
15.8911748172785));
#135344=CARTESIAN_POINT('Ctrl Pts',(-16.4741163568262,18.0082839406928,
15.8955612792911));
#135345=CARTESIAN_POINT('Ctrl Pts',(-16.5134028649731,17.9344652397022,
15.8997463422483));
#135346=CARTESIAN_POINT('Ctrl Pts',(-16.5563832077405,17.8624361059901,
15.9039314052056));
#135347=CARTESIAN_POINT('Ctrl Pts',(-16.6028702262198,17.7925903668871,
15.9081164681628));
#135348=CARTESIAN_POINT('Ctrl Pts',(-16.6492791580825,17.7228619512356,
15.9122945012563));
#135349=CARTESIAN_POINT('Ctrl Pts',(-16.6991828014219,17.6553100178988,
15.9164725343498));
#135350=CARTESIAN_POINT('Ctrl Pts',(-16.7523481443525,17.5903038770304,
15.9206505674433));
#135351=CARTESIAN_POINT('Ctrl Pts',(-16.8054619536389,17.525360747198,15.9248245507318));
#135352=CARTESIAN_POINT('Ctrl Pts',(-16.8618308964002,17.4629588649887,
15.9289985340203));
#135353=CARTESIAN_POINT('Ctrl Pts',(-16.9211791819185,17.4034379176553,
15.9331725173088));
#135354=CARTESIAN_POINT('Ctrl Pts',(-16.9804837256409,17.3439608393757,
15.9373434242233));
#135355=CARTESIAN_POINT('Ctrl Pts',(-17.0427629244188,17.2873608011024,
15.9415143311377));
#135356=CARTESIAN_POINT('Ctrl Pts',(-17.1077022600073,17.2339426763762,
15.9456852380522));
#135357=CARTESIAN_POINT('Ctrl Pts',(-17.1296568733952,17.2158831402623,
15.9470953333042));
#135358=CARTESIAN_POINT('Ctrl Pts',(-17.1519152216166,17.1981869775567,
15.9485054285563));
#135359=CARTESIAN_POINT('Ctrl Pts',(-17.174464231106,17.180864983421,15.9499155238083));
#135360=CARTESIAN_POINT('Ctrl Pts',(-17.174464231106,17.180864983421,15.149955384767));
#135361=CARTESIAN_POINT('Ctrl Pts',(-17.240940630191,17.1297982704617,15.1541321162688));
#135362=CARTESIAN_POINT('Ctrl Pts',(-17.3100170700777,17.0819316454899,
15.1583088477706));
#135363=CARTESIAN_POINT('Ctrl Pts',(-17.3813512206993,17.0375370304842,
15.1624855792724));
#135364=CARTESIAN_POINT('Ctrl Pts',(-17.4526154142036,16.9931859531006,
15.1666582146703));
#135365=CARTESIAN_POINT('Ctrl Pts',(-17.5261325291112,16.9523003606111,
15.1708308500681));
#135366=CARTESIAN_POINT('Ctrl Pts',(-17.6015298591648,16.9151098937195,
15.175003485466));
#135367=CARTESIAN_POINT('Ctrl Pts',(-17.6768876681862,16.8779389209617,
15.1791739336928));
#135368=CARTESIAN_POINT('Ctrl Pts',(-17.7541233237704,16.8444594312558,
15.1833443819196));
#135369=CARTESIAN_POINT('Ctrl Pts',(-17.8328390496217,16.8148554005417,
15.1875148301464));
#135370=CARTESIAN_POINT('Ctrl Pts',(-17.9115371280723,16.7852580068011,
15.1916843433939));
#135371=CARTESIAN_POINT('Ctrl Pts',(-17.9917141871842,16.7595345078961,
15.1958538566414));
#135372=CARTESIAN_POINT('Ctrl Pts',(-18.0729532517235,16.7378204277503,
15.200023369889));
#135373=CARTESIAN_POINT('Ctrl Pts',(-18.1541984727113,16.7161047020709,
15.20419319911));
#135374=CARTESIAN_POINT('Ctrl Pts',(-18.236505414156,16.6983991159896,15.2083630283311));
#135375=CARTESIAN_POINT('Ctrl Pts',(-18.3194440819341,16.6847887279967,
15.2125328575522));
#135376=CARTESIAN_POINT('Ctrl Pts',(-18.4024695461715,16.6711640965452,
15.216707050557));
#135377=CARTESIAN_POINT('Ctrl Pts',(-18.4861276019741,16.6616432956659,
15.2208812435618));
#135378=CARTESIAN_POINT('Ctrl Pts',(-18.5699807426584,16.6562597620852,
15.2250554365667));
#135379=CARTESIAN_POINT('Ctrl Pts',(-18.6538792241245,16.6508733175387,
15.2292318866268));
#135380=CARTESIAN_POINT('Ctrl Pts',(-18.7379725403117,16.6496286017922,
15.2334083366869));
#135381=CARTESIAN_POINT('Ctrl Pts',(-18.8218232182444,16.6525068727204,
15.237584786747));
#135382=CARTESIAN_POINT('Ctrl Pts',(-18.9058197639797,16.6553901507285,
15.2417685022176));
#135383=CARTESIAN_POINT('Ctrl Pts',(-18.989572369497,16.6624107030258,15.2459522176882));
#135384=CARTESIAN_POINT('Ctrl Pts',(-19.0726489290364,16.6734979009147,
15.2501359331588));
#135385=CARTESIAN_POINT('Ctrl Pts',(-19.135836369568,16.6819307448017,15.2533180374005));
#135386=CARTESIAN_POINT('Ctrl Pts',(-19.1986328257473,16.6927150716866,
15.2565001416423));
#135387=CARTESIAN_POINT('Ctrl Pts',(-19.2608535512399,16.7058003401833,
15.259682245884));
#135388=CARTESIAN_POINT('Ctrl Pts',(-19.3426770768309,16.7230081562804,
15.263866880277));
#135389=CARTESIAN_POINT('Ctrl Pts',(-19.4238089369641,16.74426092691,15.2680515146701));
#135390=CARTESIAN_POINT('Ctrl Pts',(-19.5038189245164,16.7694884142285,
15.2722361490631));
#135391=CARTESIAN_POINT('Ctrl Pts',(-19.5837150277547,16.7946799933414,
15.2764148271471));
#135392=CARTESIAN_POINT('Ctrl Pts',(-19.6624919952645,16.8238349143801,
15.280593505231));
#135393=CARTESIAN_POINT('Ctrl Pts',(-19.7397300928959,16.8568319982967,
15.284772183315));
#135394=CARTESIAN_POINT('Ctrl Pts',(-19.8183526279172,16.8904205312279,
15.2890257612004));
#135395=CARTESIAN_POINT('Ctrl Pts',(-19.895380110122,16.92799022417,15.2932793390859));
#135396=CARTESIAN_POINT('Ctrl Pts',(-19.9703862586171,16.9693601940761,
15.2975329169713));
#135397=CARTESIAN_POINT('Ctrl Pts',(-20.0439382665611,17.0099281263885,
15.3017040309492));
#135398=CARTESIAN_POINT('Ctrl Pts',(-20.1155461950125,17.0541500666243,
15.3058751449272));
#135399=CARTESIAN_POINT('Ctrl Pts',(-20.1848301560492,17.1018077711365,
15.3100462589051));
#135400=CARTESIAN_POINT('Ctrl Pts',(-20.2540908681836,17.1494494836456,
15.3142159732255));
#135401=CARTESIAN_POINT('Ctrl Pts',(-20.3210287829504,17.2005244102481,
15.3183856875459));
#135402=CARTESIAN_POINT('Ctrl Pts',(-20.3852923626423,17.2547705827079,
15.3225554018662));
#135403=CARTESIAN_POINT('Ctrl Pts',(-20.4495536555603,17.3090148248561,
15.3267249678103));
#135404=CARTESIAN_POINT('Ctrl Pts',(-20.5111404516292,17.3664297911047,
15.3308945337543));
#135405=CARTESIAN_POINT('Ctrl Pts',(-20.5697347912254,17.4267136507039,
15.3350640996984));
#135406=CARTESIAN_POINT('Ctrl Pts',(-20.6303892355179,17.4891170164384,
15.3393802624373));
#135407=CARTESIAN_POINT('Ctrl Pts',(-20.68783651095,17.5545943914713,15.3436964251762));
#135408=CARTESIAN_POINT('Ctrl Pts',(-20.7417674193154,17.6227714301979,
15.3480125879151));
#135409=CARTESIAN_POINT('Ctrl Pts',(-20.7939415340132,17.6887276090589,
15.3521881521068));
#135410=CARTESIAN_POINT('Ctrl Pts',(-20.8428246196127,17.7572098587051,
15.3563637162985));
#135411=CARTESIAN_POINT('Ctrl Pts',(-20.8881804708299,17.8278490685774,
15.3605392804902));
#135412=CARTESIAN_POINT('Ctrl Pts',(-20.9358271382688,17.9020560970117,
15.3649257425027));
#135413=CARTESIAN_POINT('Ctrl Pts',(-20.9795805961808,17.9786432012269,
15.3693122045153));
#135414=CARTESIAN_POINT('Ctrl Pts',(-21.0192222426253,18.0571545589591,
15.3736986665278));
#135415=CARTESIAN_POINT('Ctrl Pts',(-21.0588638890698,18.1356659166914,
15.3780851285404));
#135416=CARTESIAN_POINT('Ctrl Pts',(-21.0943935591862,18.2161009664617,
15.3824715905529));
#135417=CARTESIAN_POINT('Ctrl Pts',(-21.1256522921828,18.2979833992217,
15.3868580525655));
#135418=CARTESIAN_POINT('Ctrl Pts',(-21.1596866697224,18.3871366489942,
15.3916340140292));
#135419=CARTESIAN_POINT('Ctrl Pts',(-21.188765023978,18.4782809296074,15.396409975493));
#135420=CARTESIAN_POINT('Ctrl Pts',(-21.2126811308611,18.5708907503299,
15.4011859369568));
#135421=CARTESIAN_POINT('Ctrl Pts',(-21.236499376369,18.6631216245769,15.4059423558521));
#135422=CARTESIAN_POINT('Ctrl Pts',(-21.2551974088383,18.7568058878157,
15.4106987747474));
#135423=CARTESIAN_POINT('Ctrl Pts',(-21.2686182636666,18.8514026453274,
15.4154551936427));
#135424=CARTESIAN_POINT('Ctrl Pts',(-21.2819450244393,18.9453361818536,
15.4201782651283));
#135425=CARTESIAN_POINT('Ctrl Pts',(-21.2900682365864,19.0401692636774,
15.4249013366139));
#135426=CARTESIAN_POINT('Ctrl Pts',(-21.2928821031966,19.1353535728531,
15.4296244080995));
#135427=CARTESIAN_POINT('Ctrl Pts',(-21.2936100754836,19.1599785991387,
15.4308463086469));
#135428=CARTESIAN_POINT('Ctrl Pts',(-21.2939829474075,19.1846270439602,
15.4320682091942));
#135429=CARTESIAN_POINT('Ctrl Pts',(-21.293999428374,19.2092892327452,15.4332901097416));
#135430=CARTESIAN_POINT('',(-21.2939991231355,19.2131188547121,15.3667098902285));
#135431=CARTESIAN_POINT('Ctrl Pts',(-17.174464231106,17.180864983421,15.0832685841393));
#135432=CARTESIAN_POINT('Ctrl Pts',(-17.2419505642565,17.1290224460527,
15.0874896183852));
#135433=CARTESIAN_POINT('Ctrl Pts',(-17.3119989353086,17.0805684098818,
15.0917106526312));
#135434=CARTESIAN_POINT('Ctrl Pts',(-17.3842279949674,17.0357493168762,
15.0959316868771));
#135435=CARTESIAN_POINT('Ctrl Pts',(-17.4556818847612,16.9914112270907,
15.1001074205396));
#135436=CARTESIAN_POINT('Ctrl Pts',(-17.5292694432467,16.9506306039143,
15.104283154202));
#135437=CARTESIAN_POINT('Ctrl Pts',(-17.6045968973434,16.9135995926462,
15.1084588878645));
#135438=CARTESIAN_POINT('Ctrl Pts',(-17.6811501399716,16.8759659831692,
15.1127025724022));
#135439=CARTESIAN_POINT('Ctrl Pts',(-17.7594999534078,16.8422053023395,
15.1169462569399));
#135440=CARTESIAN_POINT('Ctrl Pts',(-17.8392139784633,16.8124675370839,
15.1211899414776));
#135441=CARTESIAN_POINT('Ctrl Pts',(-17.9189280035187,16.7827297718283,
15.1254336260153));
#135442=CARTESIAN_POINT('Ctrl Pts',(-18.0000057517656,16.7570150077627,
15.129677310553));
#135443=CARTESIAN_POINT('Ctrl Pts',(-18.0820028534396,16.7354193164275,
15.1339209950906));
#135444=CARTESIAN_POINT('Ctrl Pts',(-18.1628589794658,16.7141241254443,
15.1381056294837));
#135445=CARTESIAN_POINT('Ctrl Pts',(-18.2449099711144,16.6967547916185,
15.1422902638767));
#135446=CARTESIAN_POINT('Ctrl Pts',(-18.3277397785879,16.6834413691275,
15.1464748982698));
#135447=CARTESIAN_POINT('Ctrl Pts',(-18.4104516880828,16.6701468966455,
15.1506535763537));
#135448=CARTESIAN_POINT('Ctrl Pts',(-18.4939397611591,16.66089694071,15.1548322544377));
#135449=CARTESIAN_POINT('Ctrl Pts',(-18.5777744754985,16.6557713242267,
15.1590109325216));
#135450=CARTESIAN_POINT('Ctrl Pts',(-18.6631118668416,16.6505538347517,
15.163264510407));
#135451=CARTESIAN_POINT('Ctrl Pts',(-18.7488079825292,16.6496101194126,
15.1675180882925));
#135452=CARTESIAN_POINT('Ctrl Pts',(-18.8344006857351,16.652969565798,15.1717716661779));
#135453=CARTESIAN_POINT('Ctrl Pts',(-18.9183340073688,16.6562638827597,
15.1759427801559));
#135454=CARTESIAN_POINT('Ctrl Pts',(-19.0021674095958,16.6636959811426,
15.1801138941338));
#135455=CARTESIAN_POINT('Ctrl Pts',(-19.085463479757,16.6752410559367,15.1842850081118));
#135456=CARTESIAN_POINT('Ctrl Pts',(-19.1687315991175,16.6867822566694,
15.1884547224321));
#135457=CARTESIAN_POINT('Ctrl Pts',(-19.2514622892072,16.70243362971,15.1926244367525));
#135458=CARTESIAN_POINT('Ctrl Pts',(-19.3332238803081,16.7221185762941,
15.1967941510729));
#135459=CARTESIAN_POINT('Ctrl Pts',(-19.4149825619807,16.7418028224032,
15.2009637170169));
#135460=CARTESIAN_POINT('Ctrl Pts',(-19.4957717661756,16.7655202481684,
15.205133282961));
#135461=CARTESIAN_POINT('Ctrl Pts',(-19.5751719705258,16.7931435700187,
15.209302848905));
#135462=CARTESIAN_POINT('Ctrl Pts',(-19.6573637881102,16.8217380937883,
15.2136190116439));
#135463=CARTESIAN_POINT('Ctrl Pts',(-19.7380666159158,16.8545181133117,
15.2179351743828));
#135464=CARTESIAN_POINT('Ctrl Pts',(-19.8168362586915,16.891287596088,15.2222513371218));
#135465=CARTESIAN_POINT('Ctrl Pts',(-19.8930399886387,16.9268593168303,
15.2264269013134));
#135466=CARTESIAN_POINT('Ctrl Pts',(-19.9674341519877,16.966164316944,15.2306024655051));
#135467=CARTESIAN_POINT('Ctrl Pts',(-20.0396421490695,17.0089785244977,
15.2347780296968));
#135468=CARTESIAN_POINT('Ctrl Pts',(-20.1154972004258,17.0539551758939,
15.2391644917093));
#135469=CARTESIAN_POINT('Ctrl Pts',(-20.1889389488847,17.1028045279329,
15.2435509537219));
#135470=CARTESIAN_POINT('Ctrl Pts',(-20.2595676620249,17.1552171056787,
15.2479374157344));
#135471=CARTESIAN_POINT('Ctrl Pts',(-20.3301963751651,17.2076296834245,
15.252323877747));
#135472=CARTESIAN_POINT('Ctrl Pts',(-20.3980116539333,17.2636050588652,
15.2567103397595));
#135473=CARTESIAN_POINT('Ctrl Pts',(-20.4626578964189,17.3227887096121,
15.2610968017721));
#135474=CARTESIAN_POINT('Ctrl Pts',(-20.5234100187947,17.3784072924496,
15.2652190348167));
#135475=CARTESIAN_POINT('Ctrl Pts',(-20.5816044022757,17.4370795204071,
15.2693412678613));
#135476=CARTESIAN_POINT('Ctrl Pts',(-20.6369112461388,17.498537215202,15.2734635009059));
#135477=CARTESIAN_POINT('Ctrl Pts',(-20.6921256485485,17.5598921878337,
15.2775788439313));
#135478=CARTESIAN_POINT('Ctrl Pts',(-20.7444617859859,17.6240230272318,
15.2816941869567));
#135479=CARTESIAN_POINT('Ctrl Pts',(-20.793624524071,17.6906228034315,15.2858095299821));
#135480=CARTESIAN_POINT('Ctrl Pts',(-20.8427410076366,17.7571599195604,
15.2899210011074));
#135481=CARTESIAN_POINT('Ctrl Pts',(-20.8886897335868,17.8261609852054,
15.2940324722326));
#135482=CARTESIAN_POINT('Ctrl Pts',(-20.9312146121396,17.8972846776412,
15.2981439433579));
#135483=CARTESIAN_POINT('Ctrl Pts',(-20.9737131282073,17.9683642783043,
15.3022528656552));
#135484=CARTESIAN_POINT('Ctrl Pts',(-21.0127917657825,18.0415634879279,
15.3063617879526));
#135485=CARTESIAN_POINT('Ctrl Pts',(-21.0482376124066,18.1165118669796,
15.3104707102499));
#135486=CARTESIAN_POINT('Ctrl Pts',(-21.0836728562224,18.1914378269505,
15.3145784034579));
#135487=CARTESIAN_POINT('Ctrl Pts',(-21.1154772648512,18.2681114878987,
15.3186860966658));
#135488=CARTESIAN_POINT('Ctrl Pts',(-21.1434845038954,18.3461390715913,
15.3227937898737));
#135489=CARTESIAN_POINT('Ctrl Pts',(-21.1715053065244,18.4242044431482,
15.3269034723903));
#135490=CARTESIAN_POINT('Ctrl Pts',(-21.1957251016689,18.5036246009545,
15.331013154907));
#135491=CARTESIAN_POINT('Ctrl Pts',(-21.2160265895475,18.5839880313906,
15.3351228374236));
#135492=CARTESIAN_POINT('Ctrl Pts',(-21.2363332616047,18.6643719833958,
15.339233569387));
#135493=CARTESIAN_POINT('Ctrl Pts',(-21.2527195357628,18.7456992225568,
15.3433443013503));
#135494=CARTESIAN_POINT('Ctrl Pts',(-21.2651191757883,18.827547632741,15.3474550333136));
#135495=CARTESIAN_POINT('Ctrl Pts',(-21.2775338661873,18.9094953884813,
15.3515707547807));
#135496=CARTESIAN_POINT('Ctrl Pts',(-21.2859522113273,18.9919651056503,
15.3556864762478));
#135497=CARTESIAN_POINT('Ctrl Pts',(-21.2903598951031,19.0745299054426,
15.3598021977149));
#135498=CARTESIAN_POINT('Ctrl Pts',(-21.292825799276,19.1207212600627,15.3621047618861));
#135499=CARTESIAN_POINT('Ctrl Pts',(-21.294037342402,19.1669423575626,15.3644073260573));
#135500=CARTESIAN_POINT('Ctrl Pts',(-21.2939991231355,19.2131188547121,
15.3667098902285));
#135501=CARTESIAN_POINT('Ctrl Pts',(-21.2956374879243,19.2131202107504,
15.3667098902285));
#135502=CARTESIAN_POINT('Ctrl Pts',(-21.2969229026965,19.3573559385303,
15.3738974629702));
#135503=CARTESIAN_POINT('Ctrl Pts',(-21.2201492855026,20.3509180416766,
15.4234769712724));
#135504=CARTESIAN_POINT('Ctrl Pts',(-19.9200692925299,21.9960549863024,
15.515448415135));
#135505=CARTESIAN_POINT('Ctrl Pts',(-17.0342063134898,21.7157940168225,
15.6426242218164));
#135506=CARTESIAN_POINT('Ctrl Pts',(-15.7555914341564,19.2304392007512,
15.7652176520219));
#135507=CARTESIAN_POINT('Ctrl Pts',(-16.5753465329547,17.6447069007991,
15.845419146667));
#135508=CARTESIAN_POINT('Ctrl Pts',(-17.172599350298,17.1784745189047,15.8832287057516));
#135509=CARTESIAN_POINT('Origin',(-18.734,19.211,-1.76670989022852));
#135510=CARTESIAN_POINT('',(-17.174464231106,17.180864983421,16.749817664185));
#135511=CARTESIAN_POINT('',(-17.174464231106,17.180864983421,16.6833822560226));
#135512=CARTESIAN_POINT('',(-17.174464231106,17.180864983421,-1.76670989022852));
#135513=CARTESIAN_POINT('',(-21.2939992944986,19.2129005700935,16.2332901098004));
#135514=CARTESIAN_POINT('Ctrl Pts',(-21.2939992944986,19.2129005700935,
16.2332901098004));
#135515=CARTESIAN_POINT('Ctrl Pts',(-21.2939272486892,19.3099436741152,
16.2381006886061));
#135516=CARTESIAN_POINT('Ctrl Pts',(-21.2883332378637,19.4067618611679,
16.2429112674118));
#135517=CARTESIAN_POINT('Ctrl Pts',(-21.2773175036261,19.5027808694022,
16.2477218462175));
#135518=CARTESIAN_POINT('Ctrl Pts',(-21.2661096544807,19.6004744535223,
16.2526163217372));
#135519=CARTESIAN_POINT('Ctrl Pts',(-21.2492893600036,19.6973405506026,
16.2575107972568));
#135520=CARTESIAN_POINT('Ctrl Pts',(-21.2270132516536,19.792794574639,16.2624052727765));
#135521=CARTESIAN_POINT('Ctrl Pts',(-21.2047371433036,19.8882485986755,
16.2672997482961));
#135522=CARTESIAN_POINT('Ctrl Pts',(-21.1770053785922,19.9822904288902,
16.2721942238158));
#135523=CARTESIAN_POINT('Ctrl Pts',(-21.1440235064311,20.074357804418,16.2770886993354));
#135524=CARTESIAN_POINT('Ctrl Pts',(-21.1158249638011,20.1530727360925,
16.2812733337285));
#135525=CARTESIAN_POINT('Ctrl Pts',(-21.0837134704203,20.2305511910393,
16.2854579681215));
#135526=CARTESIAN_POINT('Ctrl Pts',(-21.0478172393665,20.3063765484118,
16.2896426025146));
#135527=CARTESIAN_POINT('Ctrl Pts',(-21.0119721021545,20.3820939777732,
16.2938212805985));
#135528=CARTESIAN_POINT('Ctrl Pts',(-20.9723531229123,20.4561625710811,
16.2979999586825));
#135529=CARTESIAN_POINT('Ctrl Pts',(-20.9291375533232,20.5281830252437,
16.3021786367664));
#135530=CARTESIAN_POINT('Ctrl Pts',(-20.8851473757077,20.601494394287,16.3064322146518));
#135531=CARTESIAN_POINT('Ctrl Pts',(-20.8374305643565,20.6726830222908,
16.3106857925373));
#135532=CARTESIAN_POINT('Ctrl Pts',(-20.7862244101177,20.7413512572338,
16.3149393704227));
#135533=CARTESIAN_POINT('Ctrl Pts',(-20.7360109870995,20.8086882244473,
16.3191104844007));
#135534=CARTESIAN_POINT('Ctrl Pts',(-20.6824425969519,20.873601266221,16.3232815983786));
#135535=CARTESIAN_POINT('Ctrl Pts',(-20.6257872198946,20.9357437823176,
16.3274527123566));
#135536=CARTESIAN_POINT('Ctrl Pts',(-20.5691508540963,20.9978654458928,
16.331622426677));
#135537=CARTESIAN_POINT('Ctrl Pts',(-20.5094298683183,21.0572180904716,
16.3357921409973));
#135538=CARTESIAN_POINT('Ctrl Pts',(-20.4469316957122,21.1134891605011,
16.3399618553177));
#135539=CARTESIAN_POINT('Ctrl Pts',(-20.3844357470594,21.1697582281645,
16.3441314212617));
#135540=CARTESIAN_POINT('Ctrl Pts',(-20.3191631505145,21.2229456321213,
16.3483009872058));
#135541=CARTESIAN_POINT('Ctrl Pts',(-20.2514562536424,21.2727775142535,
16.3524705531498));
#135542=CARTESIAN_POINT('Ctrl Pts',(-20.1813688658018,21.3243614238873,
16.3567867158888));
#135543=CARTESIAN_POINT('Ctrl Pts',(-20.1086732374466,21.372349148503,16.3611028786277));
#135544=CARTESIAN_POINT('Ctrl Pts',(-20.0337823603681,21.4164853923062,
16.3654190413666));
#135545=CARTESIAN_POINT('Ctrl Pts',(-19.9613310457333,21.4591839026097,
16.3695946055583));
#135546=CARTESIAN_POINT('Ctrl Pts',(-19.8868257455395,21.498277825633,16.37377016975));
#135547=CARTESIAN_POINT('Ctrl Pts',(-19.8106643175712,21.5335834640049,
16.3779457339416));
#135548=CARTESIAN_POINT('Ctrl Pts',(-19.7306561569328,21.5706723062398,
16.3823321959542));
#135549=CARTESIAN_POINT('Ctrl Pts',(-19.6488207114389,21.6035798961264,
16.3867186579667));
#135550=CARTESIAN_POINT('Ctrl Pts',(-19.565639342473,21.6321517928562,16.3911051199793));
#135551=CARTESIAN_POINT('Ctrl Pts',(-19.4824579735071,21.6607236895861,
16.3954915819918));
#135552=CARTESIAN_POINT('Ctrl Pts',(-19.3979312597773,21.6849598063577,
16.3998780440043));
#135553=CARTESIAN_POINT('Ctrl Pts',(-19.3125527301391,21.7047675790756,
16.4042645060169));
#135554=CARTESIAN_POINT('Ctrl Pts',(-19.2311025932108,21.7236639668085,
16.4084491404099));
#135555=CARTESIAN_POINT('Ctrl Pts',(-19.1485741315075,21.7386009007969,
16.412633774803));
#135556=CARTESIAN_POINT('Ctrl Pts',(-19.0653870565367,21.7494606789864,
16.416818409196));
#135557=CARTESIAN_POINT('Ctrl Pts',(-18.9823183880706,21.7603049996257,
16.42099708728));
#135558=CARTESIAN_POINT('Ctrl Pts',(-18.8985934206773,21.7670836326581,
16.4251757653639));
#135559=CARTESIAN_POINT('Ctrl Pts',(-18.81464384804,21.769729483508,16.4293544434479));
#135560=CARTESIAN_POINT('Ctrl Pts',(-18.7291895396467,21.7724227593329,
16.4336080213333));
#135561=CARTESIAN_POINT('Ctrl Pts',(-18.6435029643767,21.770833526475,16.4378615992187));
#135562=CARTESIAN_POINT('Ctrl Pts',(-18.5580469256855,21.7649460674884,
16.4421151771042));
#135563=CARTESIAN_POINT('Ctrl Pts',(-18.4742476190581,21.7591727483826,
16.4462862910821));
#135564=CARTESIAN_POINT('Ctrl Pts',(-18.390670470056,21.7492664079889,16.4504574050601));
#135565=CARTESIAN_POINT('Ctrl Pts',(-18.3077519672383,21.7352647671286,
16.454628519038));
#135566=CARTESIAN_POINT('Ctrl Pts',(-18.224861288525,21.7212678246541,16.4587982333584));
#135567=CARTESIAN_POINT('Ctrl Pts',(-18.1426292702904,21.7031783874643,
16.4629679476788));
#135568=CARTESIAN_POINT('Ctrl Pts',(-18.0614851300253,21.6810857777945,
16.4671376619991));
#135569=CARTESIAN_POINT('Ctrl Pts',(-17.980343877217,21.6589939542747,16.4713072279432));
#135570=CARTESIAN_POINT('Ctrl Pts',(-17.9002908690615,21.6328993631756,
16.4754767938872));
#135571=CARTESIAN_POINT('Ctrl Pts',(-17.8217416831406,21.6029416304168,
16.4796463598313));
#135572=CARTESIAN_POINT('Ctrl Pts',(-17.7404308047436,21.5719306207309,
16.4839625225702));
#135573=CARTESIAN_POINT('Ctrl Pts',(-17.6607319577168,21.5367799467921,
16.4882786853091));
#135574=CARTESIAN_POINT('Ctrl Pts',(-17.5830833500456,21.4976986825679,
16.492594848048));
#135575=CARTESIAN_POINT('Ctrl Pts',(-17.5079641376021,21.4598904864152,
16.4967704122397));
#135576=CARTESIAN_POINT('Ctrl Pts',(-17.4347640291968,21.4184041187291,
16.5009459764314));
#135577=CARTESIAN_POINT('Ctrl Pts',(-17.363852838121,21.3734746830413,16.5051215406231));
#135578=CARTESIAN_POINT('Ctrl Pts',(-17.2893600913592,21.3262759683666,
16.5095080026356));
#135579=CARTESIAN_POINT('Ctrl Pts',(-17.2173940414898,21.2752775637101,
16.5138944646481));
#135580=CARTESIAN_POINT('Ctrl Pts',(-17.1483451005789,21.2208006219378,
16.5182809266607));
#135581=CARTESIAN_POINT('Ctrl Pts',(-17.079296159668,21.1663236801655,16.5226673886732));
#135582=CARTESIAN_POINT('Ctrl Pts',(-17.0131647139457,21.1083686408955,
16.5270538506858));
#135583=CARTESIAN_POINT('Ctrl Pts',(-16.9502957329767,21.047300380603,16.5314403126983));
#135584=CARTESIAN_POINT('Ctrl Pts',(-16.8903194470162,20.9890419614914,
16.5356249470914));
#135585=CARTESIAN_POINT('Ctrl Pts',(-16.8330887583091,20.9277336646776,
16.5398095814844));
#135586=CARTESIAN_POINT('Ctrl Pts',(-16.7789298175348,20.8636646912291,
16.5439942158775));
#135587=CARTESIAN_POINT('Ctrl Pts',(-16.7248479653092,20.7996869120342,
16.5481728939614));
#135588=CARTESIAN_POINT('Ctrl Pts',(-16.6738294707905,20.7329566097131,
16.5523515720454));
#135589=CARTESIAN_POINT('Ctrl Pts',(-16.6261644175017,20.6638004533156,
16.5565302501293));
#135590=CARTESIAN_POINT('Ctrl Pts',(-16.5776450023889,20.5934047225163,
16.5607838280147));
#135591=CARTESIAN_POINT('Ctrl Pts',(-16.5326007777017,20.520495651305,16.5650374059002));
#135592=CARTESIAN_POINT('Ctrl Pts',(-16.4912954660574,20.445453876592,16.5692909837856));
#135593=CARTESIAN_POINT('Ctrl Pts',(-16.4507909384799,20.3718669331139,
16.5734620977636));
#135594=CARTESIAN_POINT('Ctrl Pts',(-16.4138818774498,20.2962296630071,
16.5776332117415));
#135595=CARTESIAN_POINT('Ctrl Pts',(-16.3807728287042,20.2189295016393,
16.5818043257195));
#135596=CARTESIAN_POINT('Ctrl Pts',(-16.3476748900196,20.1416552790873,
16.5859740400399));
#135597=CARTESIAN_POINT('Ctrl Pts',(-16.3183746121639,20.0627196959934,
16.5901437543602));
#135598=CARTESIAN_POINT('Ctrl Pts',(-16.2930292165598,19.9825320047743,
16.5943134686806));
#135599=CARTESIAN_POINT('Ctrl Pts',(-16.2676847228535,19.9023471669774,
16.5984830346247));
#135600=CARTESIAN_POINT('Ctrl Pts',(-16.2462949694201,19.8209107485429,
16.6026526005687));
#135601=CARTESIAN_POINT('Ctrl Pts',(-16.2289674972205,19.7386477613125,
16.6068221665128));
#135602=CARTESIAN_POINT('Ctrl Pts',(-16.2110308124741,19.6534925089336,
16.6111383292517));
#135603=CARTESIAN_POINT('Ctrl Pts',(-16.1974474922546,19.5674519980822,
16.6154544919906));
#135604=CARTESIAN_POINT('Ctrl Pts',(-16.1882789321129,19.4810078600996,
16.6197706547295));
#135605=CARTESIAN_POINT('Ctrl Pts',(-16.1794090368535,19.3973796308195,
16.6239462189212));
#135606=CARTESIAN_POINT('Ctrl Pts',(-16.1746706763875,19.3133741398416,
16.6281217831129));
#135607=CARTESIAN_POINT('Ctrl Pts',(-16.1740663387713,19.2294295987024,
16.6322973473046));
#135608=CARTESIAN_POINT('Ctrl Pts',(-16.1734314774988,19.1412452183496,
16.6366838093171));
#135609=CARTESIAN_POINT('Ctrl Pts',(-16.1773592072922,19.0531286901045,
16.6410702713296));
#135610=CARTESIAN_POINT('Ctrl Pts',(-16.1857908120614,18.965582122686,16.6454567333422));
#135611=CARTESIAN_POINT('Ctrl Pts',(-16.1942224168306,18.8780355552674,
16.6498431953547));
#135612=CARTESIAN_POINT('Ctrl Pts',(-16.2071577359856,18.7910595113906,
16.6542296573673));
#135613=CARTESIAN_POINT('Ctrl Pts',(-16.2244766916358,18.7051415565825,
16.6586161193798));
#135614=CARTESIAN_POINT('Ctrl Pts',(-16.240994821372,18.6231964351303,16.6627997520462));
#135615=CARTESIAN_POINT('Ctrl Pts',(-16.2615616142013,18.5419087704143,
16.6669833847125));
#135616=CARTESIAN_POINT('Ctrl Pts',(-16.2861104910119,18.4617090339621,
16.6711670173789));
#135617=CARTESIAN_POINT('Ctrl Pts',(-16.3106270618205,18.3816148393183,
16.6753451444392));
#135618=CARTESIAN_POINT('Ctrl Pts',(-16.339115179776,18.3026061663184,16.6795232714995));
#135619=CARTESIAN_POINT('Ctrl Pts',(-16.3714572466673,18.2251035862349,
16.6837013985598));
#135620=CARTESIAN_POINT('Ctrl Pts',(-16.4037664575567,18.1476797402942,
16.6878752811));
#135621=CARTESIAN_POINT('Ctrl Pts',(-16.4399216659457,18.0717593708794,
16.6920491636403));
#135622=CARTESIAN_POINT('Ctrl Pts',(-16.4797558270827,17.9977468488117,
16.6962230461805));
#135623=CARTESIAN_POINT('Ctrl Pts',(-16.5195614728604,17.9237873087472,
16.7003939408391));
#135624=CARTESIAN_POINT('Ctrl Pts',(-16.5630406213955,17.85173330636,16.7045648354977));
#135625=CARTESIAN_POINT('Ctrl Pts',(-16.6099791482389,17.7819669628438,
16.7087357301563));
#135626=CARTESIAN_POINT('Ctrl Pts',(-16.6569061252189,17.7122177862859,
16.7129055985095));
#135627=CARTESIAN_POINT('Ctrl Pts',(-16.7072905385225,17.6447555353964,
16.7170754668627));
#135628=CARTESIAN_POINT('Ctrl Pts',(-16.7608741705703,17.579934562552,16.7212453352159));
#135629=CARTESIAN_POINT('Ctrl Pts',(-16.814450725419,17.5151221511081,16.7254146528227));
#135630=CARTESIAN_POINT('Ctrl Pts',(-16.8712253612617,17.4529506748475,
16.7295839704296));
#135631=CARTESIAN_POINT('Ctrl Pts',(-16.9308997149285,17.3937412506814,
16.7337532880365));
#135632=CARTESIAN_POINT('Ctrl Pts',(-16.9906010256115,17.3345050795242,
16.7379244890716));
#135633=CARTESIAN_POINT('Ctrl Pts',(-17.0532043372424,17.2782339503866,
16.7420956901067));
#135634=CARTESIAN_POINT('Ctrl Pts',(-17.1183753223192,17.2252112647946,
16.7462668911418));
#135635=CARTESIAN_POINT('Ctrl Pts',(-17.1368677880835,17.2101659160572,
16.7474504821562));
#135636=CARTESIAN_POINT('Ctrl Pts',(-17.155566790538,17.1953818674044,16.7486340731706));
#135637=CARTESIAN_POINT('Ctrl Pts',(-17.174464231106,17.180864983421,16.749817664185));
#135638=CARTESIAN_POINT('Ctrl Pts',(-17.174464231106,17.180864983421,15.9499155238083));
#135639=CARTESIAN_POINT('Ctrl Pts',(-17.2411397248561,17.1296453273081,
15.9540850549449));
#135640=CARTESIAN_POINT('Ctrl Pts',(-17.3103588008463,17.0817002942196,
15.9582545860814));
#135641=CARTESIAN_POINT('Ctrl Pts',(-17.3817622485653,17.0372812823194,
15.962424117218));
#135642=CARTESIAN_POINT('Ctrl Pts',(-17.453169987322,16.9928596010292,15.9665938989253));
#135643=CARTESIAN_POINT('Ctrl Pts',(-17.5267619671467,16.95196460357,15.9707636806326));
#135644=CARTESIAN_POINT('Ctrl Pts',(-17.6021517731608,16.9148032333006,
15.9749334623399));
#135645=CARTESIAN_POINT('Ctrl Pts',(-17.6776197620901,16.8776033248731,
15.9791075683147));
#135646=CARTESIAN_POINT('Ctrl Pts',(-17.7548888870243,16.8441449798714,
15.9832816742895));
#135647=CARTESIAN_POINT('Ctrl Pts',(-17.8335504480885,16.8145879727262,
15.9874557802643));
#135648=CARTESIAN_POINT('Ctrl Pts',(-17.9122534362687,16.7850153993814,
15.9916320845323));
#135649=CARTESIAN_POINT('Ctrl Pts',(-17.992349882587,16.7593483961333,15.9958083888003));
#135650=CARTESIAN_POINT('Ctrl Pts',(-18.0734158610802,16.7376968250116,
15.9999846930683));
#135651=CARTESIAN_POINT('Ctrl Pts',(-18.1546241977047,16.7160072320557,
16.0041683312497));
#135652=CARTESIAN_POINT('Ctrl Pts',(-18.2368050172129,16.6983472540206,
16.0083519694312));
#135653=CARTESIAN_POINT('Ctrl Pts',(-18.3195243135909,16.6847755631426,
16.0125356076127));
#135654=CARTESIAN_POINT('Ctrl Pts',(-18.3867591839236,16.6737443900507,
16.0159361003993));
#135655=CARTESIAN_POINT('Ctrl Pts',(-18.4543495507435,16.6654131903478,
16.0193365931859));
#135656=CARTESIAN_POINT('Ctrl Pts',(-18.5220617179684,16.6597880988421,
16.0227370859726));
#135657=CARTESIAN_POINT('Ctrl Pts',(-18.6053880714047,16.6528658811356,
16.0269217203656));
#135658=CARTESIAN_POINT('Ctrl Pts',(-18.6892089831255,16.6500174172729,
16.0311063547587));
#135659=CARTESIAN_POINT('Ctrl Pts',(-18.7730921344107,16.6512984929826,
16.0352909891517));
#135660=CARTESIAN_POINT('Ctrl Pts',(-18.856855888413,16.6525777452396,16.0394696672357));
#135661=CARTESIAN_POINT('Ctrl Pts',(-18.9406812499664,16.6579748547684,
16.0436483453196));
#135662=CARTESIAN_POINT('Ctrl Pts',(-19.0241313606307,16.6674937991861,
16.0478270234036));
#135663=CARTESIAN_POINT('Ctrl Pts',(-19.1090772545541,16.6771833638415,
16.052080601289));
#135664=CARTESIAN_POINT('Ctrl Pts',(-19.1936338320393,16.6911440245191,
16.0563341791744));
#135665=CARTESIAN_POINT('Ctrl Pts',(-19.2773408795587,16.7093244237911,
16.0605877570599));
#135666=CARTESIAN_POINT('Ctrl Pts',(-19.359425102621,16.727152360547,16.0647588710378));
#135667=CARTESIAN_POINT('Ctrl Pts',(-19.4406919711072,16.7490377781069,
16.0689299850158));
#135668=CARTESIAN_POINT('Ctrl Pts',(-19.5207150357479,16.7748802466775,
16.0731010989937));
#135669=CARTESIAN_POINT('Ctrl Pts',(-19.6007112478765,16.8007140435582,
16.0772708133141));
#135670=CARTESIAN_POINT('Ctrl Pts',(-19.6794640476566,16.8305021131095,
16.0814405276345));
#135671=CARTESIAN_POINT('Ctrl Pts',(-19.7565616407634,16.8640940174691,
16.0856102419549));
#135672=CARTESIAN_POINT('Ctrl Pts',(-19.8336564904069,16.8976847264846,
16.0897798078989));
#135673=CARTESIAN_POINT('Ctrl Pts',(-19.9090958290849,16.9350788166485,
16.0939493738429));
#135674=CARTESIAN_POINT('Ctrl Pts',(-19.982488631727,16.9760780469,16.098118939787));
#135675=CARTESIAN_POINT('Ctrl Pts',(-20.0584618347703,17.0185187595092,
16.1024351025259));
#135676=CARTESIAN_POINT('Ctrl Pts',(-20.1322414512869,17.0648225852951,
16.1067512652648));
#135677=CARTESIAN_POINT('Ctrl Pts',(-20.2034241040029,17.1147192929917,
16.1110674280037));
#135678=CARTESIAN_POINT('Ctrl Pts',(-20.2722879892937,17.1629906206833,
16.1152429921954));
#135679=CARTESIAN_POINT('Ctrl Pts',(-20.3387211617813,17.2146240223489,
16.1194185563871));
#135680=CARTESIAN_POINT('Ctrl Pts',(-20.4023916835425,17.2693333987818,
16.1235941205788));
#135681=CARTESIAN_POINT('Ctrl Pts',(-20.4692780519956,17.3268060157591,
16.1279805825913));
#135682=CARTESIAN_POINT('Ctrl Pts',(-20.5331149297309,17.3876731058187,
16.1323670446039));
#135683=CARTESIAN_POINT('Ctrl Pts',(-20.5935624370342,17.4515604464003,
16.1367535066164));
#135684=CARTESIAN_POINT('Ctrl Pts',(-20.6540099443375,17.5154477869819,
16.141139968629));
#135685=CARTESIAN_POINT('Ctrl Pts',(-20.7110677625942,17.5823548872471,
16.1455264306415));
#135686=CARTESIAN_POINT('Ctrl Pts',(-20.764447298501,17.6518708302357,16.149912892654));
#135687=CARTESIAN_POINT('Ctrl Pts',(-20.8154455601759,17.7182856499018,
16.1541036735168));
#135688=CARTESIAN_POINT('Ctrl Pts',(-20.8632791399794,17.7873320135741,
16.1582944543796));
#135689=CARTESIAN_POINT('Ctrl Pts',(-20.9076654294934,17.8586765917041,
16.1624852352424));
#135690=CARTESIAN_POINT('Ctrl Pts',(-20.9519891627481,17.929920619642,16.1666701097864));
#135691=CARTESIAN_POINT('Ctrl Pts',(-20.9928750133147,18.0034560458724,
16.1708549843304));
#135692=CARTESIAN_POINT('Ctrl Pts',(-21.0300812471761,18.0789174471947,
16.1750398588744));
#135693=CARTESIAN_POINT('Ctrl Pts',(-21.0672460755937,18.1542948703099,
16.1792200762261));
#135694=CARTESIAN_POINT('Ctrl Pts',(-21.1007392197539,18.2315936031769,
16.1834002935778));
#135695=CARTESIAN_POINT('Ctrl Pts',(-21.1303635397438,18.310421416318,16.1875805109295));
#135696=CARTESIAN_POINT('Ctrl Pts',(-21.1599640139561,18.3891857778594,
16.1917573634602));
#135697=CARTESIAN_POINT('Ctrl Pts',(-21.1857016914127,18.4694763469324,
16.1959342159909));
#135698=CARTESIAN_POINT('Ctrl Pts',(-21.2074270380287,18.550879793107,16.2001110685216));
#135699=CARTESIAN_POINT('Ctrl Pts',(-21.2291418983469,18.6322439478127,
16.2042859049869));
#135700=CARTESIAN_POINT('Ctrl Pts',(-21.2468481598048,18.7147194701813,
16.2084607414522));
#135701=CARTESIAN_POINT('Ctrl Pts',(-21.2604461548154,18.7978779516678,
16.2126355779175));
#135702=CARTESIAN_POINT('Ctrl Pts',(-21.2740449836496,18.881041532398,16.2168106703821));
#135703=CARTESIAN_POINT('Ctrl Pts',(-21.2835349604935,18.9648877054714,
16.2209857628466));
#135704=CARTESIAN_POINT('Ctrl Pts',(-21.2888677421723,19.0489789519614,
16.2251608553112));
#135705=CARTESIAN_POINT('Ctrl Pts',(-21.2923288662564,19.1035565169218,
16.227870606798));
#135706=CARTESIAN_POINT('Ctrl Pts',(-21.2940398771788,19.1582371483247,
16.2305803582847));
#135707=CARTESIAN_POINT('Ctrl Pts',(-21.293999294499,19.2129005695107,16.2332901097715));
#135708=CARTESIAN_POINT('',(-21.2939994369002,19.2093020392337,16.1667098902285));
#135709=CARTESIAN_POINT('Ctrl Pts',(-17.172599350298,17.1784745189047,15.8832287057516));
#135710=CARTESIAN_POINT('Ctrl Pts',(-17.2449841473338,17.1219689062814,
15.8878110822275));
#135711=CARTESIAN_POINT('Ctrl Pts',(-18.0187464993596,16.585086496338,15.9347853942639));
#135712=CARTESIAN_POINT('Ctrl Pts',(-20.0538051846353,16.4867742534768,
16.0241516418607));
#135713=CARTESIAN_POINT('Ctrl Pts',(-21.2452321357866,18.1548349245933,
16.1140629935438));
#135714=CARTESIAN_POINT('Ctrl Pts',(-21.2975540665632,19.1065231701483,
16.1615824096664));
#135715=CARTESIAN_POINT('Ctrl Pts',(-21.2967674646518,19.2093002032948,
16.1667098902285));
#135716=CARTESIAN_POINT('Ctrl Pts',(-21.2939994369002,19.2093020392337,
16.1667098902285));
#135717=CARTESIAN_POINT('Ctrl Pts',(-21.2940542005915,19.2918687402816,
16.1708335669039));
#135718=CARTESIAN_POINT('Ctrl Pts',(-21.2901102644712,19.37459277435,16.1749572435793));
#135719=CARTESIAN_POINT('Ctrl Pts',(-21.282148407848,19.4570481489096,16.1790809202548));
#135720=CARTESIAN_POINT('Ctrl Pts',(-21.2741500199359,19.5398818524497,
16.1832235175451));
#135721=CARTESIAN_POINT('Ctrl Pts',(-21.2620966823448,19.6224439445467,
16.1873661148355));
#135722=CARTESIAN_POINT('Ctrl Pts',(-21.2460219433305,19.7043008779902,
16.1915087121259));
#135723=CARTESIAN_POINT('Ctrl Pts',(-21.23005430851,19.7856124078128,16.1956237077524));
#135724=CARTESIAN_POINT('Ctrl Pts',(-21.2101187777554,19.8662276743518,
16.1997387033789));
#135725=CARTESIAN_POINT('Ctrl Pts',(-21.1863001253011,19.9457272251988,
16.2038536990054));
#135726=CARTESIAN_POINT('Ctrl Pts',(-21.1624916905597,20.0251926723701,
16.2079669293832));
#135727=CARTESIAN_POINT('Ctrl Pts',(-21.13480357533,20.1035429002386,16.2120801597611));
#135728=CARTESIAN_POINT('Ctrl Pts',(-21.1033710027996,20.1803714721883,
16.2161933901389));
#135729=CARTESIAN_POINT('Ctrl Pts',(-21.0719418753925,20.2571916234494,
16.2203061696919));
#135730=CARTESIAN_POINT('Ctrl Pts',(-21.0367692860285,20.3324900117991,
16.2244189492448));
#135731=CARTESIAN_POINT('Ctrl Pts',(-20.998036835518,20.405879578626,16.2285317287978));
#135732=CARTESIAN_POINT('Ctrl Pts',(-20.9588192445656,20.48018838104,16.2326960226666));
#135733=CARTESIAN_POINT('Ctrl Pts',(-20.9159522062818,20.5525397612551,
16.2368603165354));
#135734=CARTESIAN_POINT('Ctrl Pts',(-20.8696736494983,20.6225587351713,
16.2410246104042));
#135735=CARTESIAN_POINT('Ctrl Pts',(-20.8239074514183,20.6918025157111,
16.2451428005837));
#135736=CARTESIAN_POINT('Ctrl Pts',(-20.7748052350545,20.7587649302322,
16.2492609907631));
#135737=CARTESIAN_POINT('Ctrl Pts',(-20.7226388747276,20.823115202435,16.2533791809425));
#135738=CARTESIAN_POINT('Ctrl Pts',(-20.6695965003383,20.8885460894827,
16.257566526656));
#135739=CARTESIAN_POINT('Ctrl Pts',(-20.6133864683218,20.9512759179512,
16.2617538723695));
#135740=CARTESIAN_POINT('Ctrl Pts',(-20.5543334369044,21.0109961606869,
16.265941218083));
#135741=CARTESIAN_POINT('Ctrl Pts',(-20.495280405487,21.0707164034227,16.2701285637965));
#135742=CARTESIAN_POINT('Ctrl Pts',(-20.4333847973435,21.1274267716985,
16.2743159095101));
#135743=CARTESIAN_POINT('Ctrl Pts',(-20.369004471075,21.1808630357374,16.2785032552236));
#135744=CARTESIAN_POINT('Ctrl Pts',(-20.3046658312848,21.2342646996153,
16.2826878896166));
#135745=CARTESIAN_POINT('Ctrl Pts',(-20.2375884427955,21.2846103343966,
16.2868725240096));
#135746=CARTESIAN_POINT('Ctrl Pts',(-20.16809472922,21.3316065895454,16.2910571584027));
#135747=CARTESIAN_POINT('Ctrl Pts',(-20.0986999313442,21.378535951342,16.2952358364866));
#135748=CARTESIAN_POINT('Ctrl Pts',(-20.0268960178075,21.4221251476138,
16.2994145145706));
#135749=CARTESIAN_POINT('Ctrl Pts',(-19.9530388079931,21.4621206952553,
16.3035931926545));
#135750=CARTESIAN_POINT('Ctrl Pts',(-19.8778577607731,21.502833134344,16.30784677054));
#135751=CARTESIAN_POINT('Ctrl Pts',(-19.8005494535681,21.5398215173808,
16.3121003484254));
#135752=CARTESIAN_POINT('Ctrl Pts',(-19.7215205448428,21.5728643427414,
16.3163539263108));
#135753=CARTESIAN_POINT('Ctrl Pts',(-19.6440237657255,21.6052665684546,
16.3205250402888));
#135754=CARTESIAN_POINT('Ctrl Pts',(-19.56487294815,21.6338746703222,16.3246961542667));
#135755=CARTESIAN_POINT('Ctrl Pts',(-19.4844751811849,21.6585267112792,
16.3288672682447));
#135756=CARTESIAN_POINT('Ctrl Pts',(-19.404104392467,21.6831704800059,16.3330369825651));
#135757=CARTESIAN_POINT('Ctrl Pts',(-19.3224879248154,21.7038606894987,
16.3372066968854));
#135758=CARTESIAN_POINT('Ctrl Pts',(-19.2400494979671,21.7204847888774,
16.3413764112058));
#135759=CARTESIAN_POINT('Ctrl Pts',(-19.1576140046318,21.7371082966994,
16.3455459771499));
#135760=CARTESIAN_POINT('Ctrl Pts',(-19.0743570613777,21.7496658919856,
16.3497155430939));
#135761=CARTESIAN_POINT('Ctrl Pts',(-18.9907127437439,21.758096104822,16.3538851090379));
#135762=CARTESIAN_POINT('Ctrl Pts',(-18.9041275950885,21.7668227135419,
16.3582012717769));
#135763=CARTESIAN_POINT('Ctrl Pts',(-18.8171278498233,21.7711262492444,
16.3625174345158));
#135764=CARTESIAN_POINT('Ctrl Pts',(-18.7301989430817,21.7709971781169,
16.3668335972547));
#135765=CARTESIAN_POINT('Ctrl Pts',(-18.646101736334,21.7708723114677,16.3710091614464));
#135766=CARTESIAN_POINT('Ctrl Pts',(-18.5620712918898,21.7665992585964,
16.3751847256381));
#135767=CARTESIAN_POINT('Ctrl Pts',(-18.478543574057,21.7582224116563,16.3793602898297));
#135768=CARTESIAN_POINT('Ctrl Pts',(-18.3907970697647,21.7494224700914,
16.3837467518423));
#135769=CARTESIAN_POINT('Ctrl Pts',(-18.3036059893692,21.7360933624401,
16.3881332138548));
#135770=CARTESIAN_POINT('Ctrl Pts',(-18.2174632822105,21.7183471676605,
16.3925196758674));
#135771=CARTESIAN_POINT('Ctrl Pts',(-18.1313205750519,21.700600972881,16.3969061378799));
#135772=CARTESIAN_POINT('Ctrl Pts',(-18.0462267834431,21.6784379108237,
16.4012925998925));
#135773=CARTESIAN_POINT('Ctrl Pts',(-17.9626538344088,21.652029514944,16.405679061905));
#135774=CARTESIAN_POINT('Ctrl Pts',(-17.8829262006443,21.6268362085053,
16.409863696298));
#135775=CARTESIAN_POINT('Ctrl Pts',(-17.8042857709966,21.5976858772392,
16.4140483306911));
#135776=CARTESIAN_POINT('Ctrl Pts',(-17.7271537286291,21.5646908432984,
16.4182329650841));
#135777=CARTESIAN_POINT('Ctrl Pts',(-17.6501314741772,21.5317427737044,
16.4224116431681));
#135778=CARTESIAN_POINT('Ctrl Pts',(-17.5746137617241,21.4949610508433,
16.426590321252));
#135779=CARTESIAN_POINT('Ctrl Pts',(-17.5010063287307,21.4545076569091,
16.4307689993359));
#135780=CARTESIAN_POINT('Ctrl Pts',(-17.4260795354015,21.4133291649619,
16.4350225772214));
#135781=CARTESIAN_POINT('Ctrl Pts',(-17.353132638384,21.3683462231051,16.4392761551068));
#135782=CARTESIAN_POINT('Ctrl Pts',(-17.2825720020051,21.3197808721241,
16.4435297329923));
#135783=CARTESIAN_POINT('Ctrl Pts',(-17.2133793212501,21.2721570552393,
16.4477008469702));
#135784=CARTESIAN_POINT('Ctrl Pts',(-17.1464815985702,21.2210887664921,
16.4518719609482));
#135785=CARTESIAN_POINT('Ctrl Pts',(-17.0822353470014,21.1668306499041,
16.4560430749261));
#135786=CARTESIAN_POINT('Ctrl Pts',(-17.0180106538829,21.1125907401512,
16.4602127892465));
#135787=CARTESIAN_POINT('Ctrl Pts',(-16.956436016035,21.0551634249198,16.4643825035668));
#135788=CARTESIAN_POINT('Ctrl Pts',(-16.8978354223938,20.9948440637971,
16.4685522178872));
#135789=CARTESIAN_POINT('Ctrl Pts',(-16.8392369140131,20.9345268490961,
16.4727217838313));
#135790=CARTESIAN_POINT('Ctrl Pts',(-16.7836125593694,20.8713181236712,
16.4768913497753));
#135791=CARTESIAN_POINT('Ctrl Pts',(-16.7312490017889,20.8055496038582,
16.4810609157193));
#135792=CARTESIAN_POINT('Ctrl Pts',(-16.6770444061212,20.7374687440227,
16.4853770784583));
#135793=CARTESIAN_POINT('Ctrl Pts',(-16.6263345016133,20.6666451485156,
16.4896932411972));
#135794=CARTESIAN_POINT('Ctrl Pts',(-16.5793900615235,20.5934818309903,
16.4940094039361));
#135795=CARTESIAN_POINT('Ctrl Pts',(-16.5339748316321,20.5227018008381,
16.4981849681278));
#135796=CARTESIAN_POINT('Ctrl Pts',(-16.4920837070573,20.4497325726924,
16.5023605323195));
#135797=CARTESIAN_POINT('Ctrl Pts',(-16.4539153402347,20.3749647521738,
16.5065360965111));
#135798=CARTESIAN_POINT('Ctrl Pts',(-16.4138191799405,20.2964205867842,
16.5109225585237));
#135799=CARTESIAN_POINT('Ctrl Pts',(-16.3778319719898,20.215891893294,16.5153090205362));
#135800=CARTESIAN_POINT('Ctrl Pts',(-16.3461262998438,20.1338538303015,
16.5196954825488));
#135801=CARTESIAN_POINT('Ctrl Pts',(-16.3144206276978,20.051815767309,16.5240819445613));
#135802=CARTESIAN_POINT('Ctrl Pts',(-16.2869966000409,19.9682689098145,
16.5284684065739));
#135803=CARTESIAN_POINT('Ctrl Pts',(-16.2639654295305,19.8837029215676,
16.5328548685864));
#135804=CARTESIAN_POINT('Ctrl Pts',(-16.2419939573158,19.803027939797,16.5370395029795));
#135805=CARTESIAN_POINT('Ctrl Pts',(-16.223938199736,19.7211252621465,16.5412241373725));
#135806=CARTESIAN_POINT('Ctrl Pts',(-16.2099316900943,19.638409834854,16.5454087717656));
#135807=CARTESIAN_POINT('Ctrl Pts',(-16.1959451169855,19.5558121427342,
16.5495874498495));
#135808=CARTESIAN_POINT('Ctrl Pts',(-16.1859964196337,19.4724044485339,
16.5537661279335));
#135809=CARTESIAN_POINT('Ctrl Pts',(-16.18016901464,19.3886155911379,16.5579448060174));
#135810=CARTESIAN_POINT('Ctrl Pts',(-16.1742371575999,19.3033248786909,
16.5621983839028));
#135811=CARTESIAN_POINT('Ctrl Pts',(-16.1725759211884,19.2176396691378,
16.5664519617883));
#135812=CARTESIAN_POINT('Ctrl Pts',(-16.1752185615464,19.1320218370347,
16.5707055396737));
#135813=CARTESIAN_POINT('Ctrl Pts',(-16.1778099691644,19.0480638736762,
16.5748766536517));
#135814=CARTESIAN_POINT('Ctrl Pts',(-16.1845398497979,18.9641711795844,
16.5790477676296));
#135815=CARTESIAN_POINT('Ctrl Pts',(-16.1953870618677,18.8807813597822,
16.5832188816076));
#135816=CARTESIAN_POINT('Ctrl Pts',(-16.2062306340507,18.7974195222395,
16.587388595928));
#135817=CARTESIAN_POINT('Ctrl Pts',(-16.221188734479,18.7145606796676,16.5915583102483));
#135818=CARTESIAN_POINT('Ctrl Pts',(-16.2401883815475,18.6326371280316,
16.5957280245687));
#135819=CARTESIAN_POINT('Ctrl Pts',(-16.2591873525271,18.5507164915872,
16.5998975905127));
#135820=CARTESIAN_POINT('Ctrl Pts',(-16.2822274794425,18.4697315278526,
16.6040671564568));
#135821=CARTESIAN_POINT('Ctrl Pts',(-16.3091849959464,18.3901028102639,
16.6082367224008));
#135822=CARTESIAN_POINT('Ctrl Pts',(-16.337090305475,18.3076744451974,16.6125528851398));
#135823=CARTESIAN_POINT('Ctrl Pts',(-16.3691934316988,18.2266999715503,
16.6168690478787));
#135824=CARTESIAN_POINT('Ctrl Pts',(-16.4053020683426,18.1476252104292,
16.6211852106176));
#135825=CARTESIAN_POINT('Ctrl Pts',(-16.4402344699458,18.0711263013345,
16.6253607748093));
#135826=CARTESIAN_POINT('Ctrl Pts',(-16.4789151719814,17.9964056357569,
16.629536339001));
#135827=CARTESIAN_POINT('Ctrl Pts',(-16.5211232637327,17.9238416763712,
16.6337119031926));
#135828=CARTESIAN_POINT('Ctrl Pts',(-16.5654631858581,17.8476126839014,
16.6380983652052));
#135829=CARTESIAN_POINT('Ctrl Pts',(-16.613695880029,17.7737644826753,16.6424848272177));
#135830=CARTESIAN_POINT('Ctrl Pts',(-16.6655152292137,17.7026993824091,
16.6468712892303));
#135831=CARTESIAN_POINT('Ctrl Pts',(-16.7173345783984,17.6316342821429,
16.6512577512428));
#135832=CARTESIAN_POINT('Ctrl Pts',(-16.7727401579415,17.5633526854597,
16.6556442132553));
#135833=CARTESIAN_POINT('Ctrl Pts',(-16.8313804354227,17.4982131503051,
16.6600306752679));
#135834=CARTESIAN_POINT('Ctrl Pts',(-16.8873083679597,17.4360865764876,
16.6642142460498));
#135835=CARTESIAN_POINT('Ctrl Pts',(-16.9463864967517,17.3765866334562,
16.6683978168317));
#135836=CARTESIAN_POINT('Ctrl Pts',(-17.0083384129123,17.3200499512547,
16.6725813876136));
#135837=CARTESIAN_POINT('Ctrl Pts',(-17.0616528763228,17.2713957196927,
16.6761816770833));
#135838=CARTESIAN_POINT('Ctrl Pts',(-17.1170948413747,17.2249357543771,
16.6797819665529));
#135839=CARTESIAN_POINT('Ctrl Pts',(-17.174464231106,17.180864983421,16.6833822560226));
#135840=CARTESIAN_POINT('Origin',(-18.734,19.211,-1.76670989022852));
#135841=CARTESIAN_POINT('',(-17.1718943031603,17.177514077948,17.549894074293));
#135842=CARTESIAN_POINT('',(-17.1769969530062,17.1841723796816,17.4833253039094));
#135843=CARTESIAN_POINT('',(-17.174464231106,17.180864983421,-1.76670989022852));
#135844=CARTESIAN_POINT('',(-21.2942631180427,19.2118355653576,17.0332901097715));
#135845=CARTESIAN_POINT('Ctrl Pts',(-21.2979002849781,19.2118367523804,
17.0332901097715));
#135846=CARTESIAN_POINT('Ctrl Pts',(-21.2980949927007,19.2575742464713,
17.0355745863224));
#135847=CARTESIAN_POINT('Ctrl Pts',(-21.2762381497003,20.1518505805258,
17.0802509984337));
#135848=CARTESIAN_POINT('Ctrl Pts',(-20.2331956316243,21.8407726550478,
17.1673193461055));
#135849=CARTESIAN_POINT('Ctrl Pts',(-17.334263528554,21.895032333938,17.2944951527869));
#135850=CARTESIAN_POINT('Ctrl Pts',(-15.7195027605925,19.4868589362738,
17.4216709594684));
#135851=CARTESIAN_POINT('Ctrl Pts',(-16.4898974650082,17.7053824456698,
17.5068039333037));
#135852=CARTESIAN_POINT('Ctrl Pts',(-17.1663500536343,17.1817661252999,
17.5495449715786));
#135853=CARTESIAN_POINT('Ctrl Pts',(-17.1718943031603,17.177514077948,17.549894074293));
#135854=CARTESIAN_POINT('Ctrl Pts',(-17.174464231106,17.180864983421,16.749817664185));
#135855=CARTESIAN_POINT('Ctrl Pts',(-17.2411414928805,17.1296439691239,
16.7539938174381));
#135856=CARTESIAN_POINT('Ctrl Pts',(-17.3102911901789,17.0817524742227,
16.7581699706911));
#135857=CARTESIAN_POINT('Ctrl Pts',(-17.3815400031077,17.0374195536383,
16.7623461239442));
#135858=CARTESIAN_POINT('Ctrl Pts',(-17.452915189634,16.9930080000153,16.7665296844155));
#135859=CARTESIAN_POINT('Ctrl Pts',(-17.5263965273637,16.9521678546901,
16.7707132448868));
#135860=CARTESIAN_POINT('Ctrl Pts',(-17.6015860289866,16.9150821882625,
16.7748968053582));
#135861=CARTESIAN_POINT('Ctrl Pts',(-17.6668572814998,16.8828884930554,
16.7785285122592));
#135862=CARTESIAN_POINT('Ctrl Pts',(-17.7334152454288,16.853523409711,16.7821602191602));
#135863=CARTESIAN_POINT('Ctrl Pts',(-17.800989527137,16.8270764572814,16.7857919260613));
#135864=CARTESIAN_POINT('Ctrl Pts',(-17.8788519953999,16.7966029554973,
16.7899765604543));
#135865=CARTESIAN_POINT('Ctrl Pts',(-17.9583538968787,16.7698914102529,
16.7941611948473));
#135866=CARTESIAN_POINT('Ctrl Pts',(-18.0390969463691,16.7471189667408,
16.7983458292404));
#135867=CARTESIAN_POINT('Ctrl Pts',(-18.1197250681226,16.7243789369834,
16.8025245073243));
#135868=CARTESIAN_POINT('Ctrl Pts',(-18.20159038985,16.7055669958483,16.8067031854083));
#135869=CARTESIAN_POINT('Ctrl Pts',(-18.2842754534885,16.6908119450595,
16.8108818634922));
#135870=CARTESIAN_POINT('Ctrl Pts',(-18.3684425874681,16.6757924205895,
16.8151354413777));
#135871=CARTESIAN_POINT('Ctrl Pts',(-18.4534586911851,16.66497683224,16.8193890192631));
#135872=CARTESIAN_POINT('Ctrl Pts',(-18.5388680958069,16.6584476420716,
16.8236425971485));
#135873=CARTESIAN_POINT('Ctrl Pts',(-18.6226216724573,16.6520450329952,
16.8278137111265));
#135874=CARTESIAN_POINT('Ctrl Pts',(-18.7067529564691,16.6497641415373,
16.8319848251044));
#135875=CARTESIAN_POINT('Ctrl Pts',(-18.7908245916081,16.6516307484483,
16.8361559390824));
#135876=CARTESIAN_POINT('Ctrl Pts',(-18.8748680156981,16.6534967290012,
16.8403256534027));
#135877=CARTESIAN_POINT('Ctrl Pts',(-18.95885137113,16.659507433716,16.8444953677231));
#135878=CARTESIAN_POINT('Ctrl Pts',(-19.0423370360802,16.6696365328467,
16.8486650820435));
#135879=CARTESIAN_POINT('Ctrl Pts',(-19.1258197302521,16.6797652715406,
16.8528346479875));
#135880=CARTESIAN_POINT('Ctrl Pts',(-19.208804312573,16.6940120570168,16.8570042139316));
#135881=CARTESIAN_POINT('Ctrl Pts',(-19.2908593851773,16.7122988123547,
16.8611737798756));
#135882=CARTESIAN_POINT('Ctrl Pts',(-19.3757994129084,16.7312285074512,
16.8654899426145));
#135883=CARTESIAN_POINT('Ctrl Pts',(-19.4597428368619,16.7544874341396,
16.8698061053535));
#135884=CARTESIAN_POINT('Ctrl Pts',(-19.5422258260851,16.781932068869,16.8741222680924));
#135885=CARTESIAN_POINT('Ctrl Pts',(-19.62202194061,16.8084826975088,16.878297832284));
#135886=CARTESIAN_POINT('Ctrl Pts',(-19.7004508845914,16.838950308513,16.8824733964757));
#135887=CARTESIAN_POINT('Ctrl Pts',(-19.777112739986,16.8731557340835,16.8866489606674));
#135888=CARTESIAN_POINT('Ctrl Pts',(-19.8576466034504,16.9090887943838,
16.8910354226799));
#135889=CARTESIAN_POINT('Ctrl Pts',(-19.9362296554815,16.9491469214588,
16.8954218846925));
#135890=CARTESIAN_POINT('Ctrl Pts',(-20.0124291551048,16.9930687802869,
16.899808346705));
#135891=CARTESIAN_POINT('Ctrl Pts',(-20.088628654728,17.036990639115,16.9041948087175));
#135892=CARTESIAN_POINT('Ctrl Pts',(-20.1624441562133,17.0847758505362,
16.9085812707301));
#135893=CARTESIAN_POINT('Ctrl Pts',(-20.2334815623277,17.1361132454422,
16.9129677327426));
#135894=CARTESIAN_POINT('Ctrl Pts',(-20.3007008312569,17.1846913445463,
16.9171184300414));
#135895=CARTESIAN_POINT('Ctrl Pts',(-20.3656920487853,17.2366370916662,
16.9212691273401));
#135896=CARTESIAN_POINT('Ctrl Pts',(-20.4280939407347,17.2917173944502,
16.9254198246388));
#135897=CARTESIAN_POINT('Ctrl Pts',(-20.4904067758308,17.3467190893862,
16.9295645982704));
#135898=CARTESIAN_POINT('Ctrl Pts',(-20.5501372744549,17.4048461509353,
16.9337093719019));
#135899=CARTESIAN_POINT('Ctrl Pts',(-20.6069541187605,17.4658229691467,
16.9378541455335));
#135900=CARTESIAN_POINT('Ctrl Pts',(-20.6637057912848,17.5267298438773,
16.9419941649009));
#135901=CARTESIAN_POINT('Ctrl Pts',(-20.7175501324578,17.5904796396565,
16.9461341842684));
#135902=CARTESIAN_POINT('Ctrl Pts',(-20.7681909845745,17.6567583719782,
16.9502742036359));
#135903=CARTESIAN_POINT('Ctrl Pts',(-20.8188004163149,17.7229959813208,
16.9544116543072));
#135904=CARTESIAN_POINT('Ctrl Pts',(-20.8662100198437,17.7917590422704,
16.9585491049784));
#135905=CARTESIAN_POINT('Ctrl Pts',(-20.9101632231195,17.8626997269368,
16.9626865556497));
#135906=CARTESIAN_POINT('Ctrl Pts',(-20.9541028768145,17.9336185425138,
16.9668227308571));
#135907=CARTESIAN_POINT('Ctrl Pts',(-20.994587999437,18.0067132510727,16.9709589060645));
#135908=CARTESIAN_POINT('Ctrl Pts',(-21.031405596239,18.0816074524906,16.9750950812719));
#135909=CARTESIAN_POINT('Ctrl Pts',(-21.0682233367814,18.1565019463047,
16.9792312726275));
#135910=CARTESIAN_POINT('Ctrl Pts',(-21.1013733182381,18.2331955257884,
16.983367463983));
#135911=CARTESIAN_POINT('Ctrl Pts',(-21.1306893947115,18.3112889656799,
16.9875036553386));
#135912=CARTESIAN_POINT('Ctrl Pts',(-21.1600333335746,18.3894566266172,
16.9916437777855));
#135913=CARTESIAN_POINT('Ctrl Pts',(-21.1855359272154,18.4690263650883,
16.9957839002324));
#135914=CARTESIAN_POINT('Ctrl Pts',(-21.2070801670876,18.549581458411,16.9999240226793));
#135915=CARTESIAN_POINT('Ctrl Pts',(-21.2286351815299,18.6301768384412,
17.0040662156583));
#135916=CARTESIAN_POINT('Ctrl Pts',(-21.2462278030767,18.7117580962757,
17.0082084086373));
#135917=CARTESIAN_POINT('Ctrl Pts',(-21.2597921942375,18.7938983438909,
17.0123506016163));
#135918=CARTESIAN_POINT('Ctrl Pts',(-21.2733789861849,18.8761742412481,
17.016499635181));
#135919=CARTESIAN_POINT('Ctrl Pts',(-21.2829242114339,18.95901050629,17.0206486687457));
#135920=CARTESIAN_POINT('Ctrl Pts',(-21.2884139728529,19.0419755778182,
17.0247977023105));
#135921=CARTESIAN_POINT('Ctrl Pts',(-21.2921595270972,19.0985809841503,
17.0276285047975));
#135922=CARTESIAN_POINT('Ctrl Pts',(-21.2940183320645,19.1552463005707,
17.0304593072845));
#135923=CARTESIAN_POINT('Ctrl Pts',(-21.2939998636668,19.2118354794421,
17.0332901097715));
#135924=CARTESIAN_POINT('',(-21.2938494856171,19.209803254918,16.9667098397541));
#135925=CARTESIAN_POINT('Ctrl Pts',(-17.174464231106,17.180864983421,16.6833822560226));
#135926=CARTESIAN_POINT('Ctrl Pts',(-17.2433977216274,17.127910749705,16.6877082654362));
#135927=CARTESIAN_POINT('Ctrl Pts',(-17.3151147415225,17.0784073959019,
16.6920342748498));
#135928=CARTESIAN_POINT('Ctrl Pts',(-17.3892304768158,17.0326531659273,
16.6963602842634));
#135929=CARTESIAN_POINT('Ctrl Pts',(-17.4606968284318,16.9885344929579,
16.7005316536578));
#135930=CARTESIAN_POINT('Ctrl Pts',(-17.5343928910415,16.947901727856,16.7047030230523));
#135931=CARTESIAN_POINT('Ctrl Pts',(-17.6099425209296,16.9109793949301,
16.7088743924467));
#135932=CARTESIAN_POINT('Ctrl Pts',(-17.6854640454202,16.8740707975692,
16.7130442100401));
#135933=CARTESIAN_POINT('Ctrl Pts',(-17.7628373549223,16.8408700929972,
16.7172140276334));
#135934=CARTESIAN_POINT('Ctrl Pts',(-17.8416620090713,16.8115557080971,
16.7213838452268));
#135935=CARTESIAN_POINT('Ctrl Pts',(-17.920480984977,16.7822434348995,16.7255533624416));
#135936=CARTESIAN_POINT('Ctrl Pts',(-18.0007506663518,16.7568170847122,
16.7297228796563));
#135937=CARTESIAN_POINT('Ctrl Pts',(-18.0820522390349,16.735406310201,16.7338923968711));
#135938=CARTESIAN_POINT('Ctrl Pts',(-18.1633723431405,16.7139906554385,
16.7380628644621));
#135939=CARTESIAN_POINT('Ctrl Pts',(-18.245724360498,16.6965925096898,16.7422333320532));
#135940=CARTESIAN_POINT('Ctrl Pts',(-18.3286773196109,16.6832908543976,
16.7464037996442));
#135941=CARTESIAN_POINT('Ctrl Pts',(-18.4117243393771,16.6699741163114,
16.7505789961432));
#135942=CARTESIAN_POINT('Ctrl Pts',(-18.4953732056763,16.6607632092122,
16.7547541926422));
#135943=CARTESIAN_POINT('Ctrl Pts',(-18.5791864016643,16.6556853912345,
16.7589293891411));
#135944=CARTESIAN_POINT('Ctrl Pts',(-18.6630563522702,16.6506041347814,
16.7631074128999));
#135945=CARTESIAN_POINT('Ctrl Pts',(-18.7470903946914,16.6496615419162,
16.7672854366587));
#135946=CARTESIAN_POINT('Ctrl Pts',(-18.8308519536333,16.6528327460705,
16.7714634604175));
#135947=CARTESIAN_POINT('Ctrl Pts',(-18.9147465871835,16.6560089884159,
16.7756481219333));
#135948=CARTESIAN_POINT('Ctrl Pts',(-18.9983674167173,16.6633120266781,
16.7798327834491));
#135949=CARTESIAN_POINT('Ctrl Pts',(-19.0812844992108,16.6746653460933,
16.7840174449649));
#135950=CARTESIAN_POINT('Ctrl Pts',(-19.102347584139,16.6775493830598,16.7850804572931));
#135951=CARTESIAN_POINT('Ctrl Pts',(-19.1233653199158,16.6806945264327,
16.7861434696212));
#135952=CARTESIAN_POINT('Ctrl Pts',(-19.1443308019264,16.6840990060965,
16.7872064819493));
#135953=CARTESIAN_POINT('Ctrl Pts',(-19.2268631251808,16.6975010168866,
16.7913911163424));
#135954=CARTESIAN_POINT('Ctrl Pts',(-19.3088917529363,16.7149756618514,
16.7955757507354));
#135955=CARTESIAN_POINT('Ctrl Pts',(-19.389983688077,16.7364726914061,16.7997603851285));
#135956=CARTESIAN_POINT('Ctrl Pts',(-19.4709601988852,16.7579391226001,
16.8039390632124));
#135957=CARTESIAN_POINT('Ctrl Pts',(-19.5510022244943,16.7834164491322,
16.8081177412964));
#135958=CARTESIAN_POINT('Ctrl Pts',(-19.6296848716229,16.8128030500508,
16.8122964193803));
#135959=CARTESIAN_POINT('Ctrl Pts',(-19.709777848653,16.842716384671,16.8165499972657));
#135960=CARTESIAN_POINT('Ctrl Pts',(-19.7884617582361,16.8766804423688,
16.8208035751512));
#135961=CARTESIAN_POINT('Ctrl Pts',(-19.8653024038484,16.9145342652139,
16.8250571530366));
#135962=CARTESIAN_POINT('Ctrl Pts',(-19.9406533436033,16.9516542178375,
16.8292282670146));
#135963=CARTESIAN_POINT('Ctrl Pts',(-20.0142314204538,16.9925142474789,
16.8333993809925));
#135964=CARTESIAN_POINT('Ctrl Pts',(-20.0856470518142,17.0369139282627,
16.8375704949705));
#135965=CARTESIAN_POINT('Ctrl Pts',(-20.1570387189699,17.081298710305,16.8417402092909));
#135966=CARTESIAN_POINT('Ctrl Pts',(-20.2262689913883,17.1292205418819,
16.8459099236112));
#135967=CARTESIAN_POINT('Ctrl Pts',(-20.2929745824341,17.1804340071486,
16.8500796379316));
#135968=CARTESIAN_POINT('Ctrl Pts',(-20.3596777998086,17.2316456500204,
16.8542492038757));
#135969=CARTESIAN_POINT('Ctrl Pts',(-20.4238561500592,17.2861484128723,
16.8584187698197));
#135970=CARTESIAN_POINT('Ctrl Pts',(-20.4851780435305,17.3436555058435,
16.8625883357638));
#135971=CARTESIAN_POINT('Ctrl Pts',(-20.5486559391275,17.4031844772608,
16.8669044985027));
#135972=CARTESIAN_POINT('Ctrl Pts',(-20.6090723898817,17.4659326132811,
16.8712206612416));
#135973=CARTESIAN_POINT('Ctrl Pts',(-20.6661012016728,17.5315402813719,
16.8755368239805));
#135974=CARTESIAN_POINT('Ctrl Pts',(-20.7212723059183,17.5950107865754,
16.8797123881722));
#135975=CARTESIAN_POINT('Ctrl Pts',(-20.7732728325614,17.6611569867926,
16.8838879523639));
#135976=CARTESIAN_POINT('Ctrl Pts',(-20.8218497444836,17.7296211003056,
16.8880635165556));
#135977=CARTESIAN_POINT('Ctrl Pts',(-20.8728801607463,17.8015431734342,
16.8924499785681));
#135978=CARTESIAN_POINT('Ctrl Pts',(-20.9201317067405,17.8760229761492,
16.8968364405806));
#135979=CARTESIAN_POINT('Ctrl Pts',(-20.9633649162028,17.9526152931618,
16.9012229025932));
#135980=CARTESIAN_POINT('Ctrl Pts',(-21.006598125665,18.0292076101744,16.9056093646057));
#135981=CARTESIAN_POINT('Ctrl Pts',(-21.0458128079223,18.1079118882384,
16.9099958266183));
#135982=CARTESIAN_POINT('Ctrl Pts',(-21.0808281256647,18.1882596866315,
16.9143822886308));
#135983=CARTESIAN_POINT('Ctrl Pts',(-21.117652895614,18.2727595393394,16.9189954255354));
#135984=CARTESIAN_POINT('Ctrl Pts',(-21.1499518315869,18.3593459986734,
16.92360856244));
#135985=CARTESIAN_POINT('Ctrl Pts',(-21.1775079602936,18.4475415217695,
16.9282216993445));
#135986=CARTESIAN_POINT('Ctrl Pts',(-21.204985218715,18.5354846144123,16.9328216326737));
#135987=CARTESIAN_POINT('Ctrl Pts',(-21.2277466226995,18.6250273148932,
16.9374215660029));
#135988=CARTESIAN_POINT('Ctrl Pts',(-21.2456232056939,18.7156729639725,
16.942021499332));
#135989=CARTESIAN_POINT('Ctrl Pts',(-21.263411741867,18.8058721596512,16.946598776793));
#135990=CARTESIAN_POINT('Ctrl Pts',(-21.2763633328307,18.897163189666,16.951176054254));
#135991=CARTESIAN_POINT('Ctrl Pts',(-21.2843593339857,18.9890376888929,
16.955753331715));
#135992=CARTESIAN_POINT('Ctrl Pts',(-21.2907392715853,19.0623435277363,
16.9594055003441));
#135993=CARTESIAN_POINT('Ctrl Pts',(-21.2939652250926,19.136020399912,16.9630576689733));
#135994=CARTESIAN_POINT('Ctrl Pts',(-21.2939997202205,19.2098031412724,
16.9667098376024));
#135995=CARTESIAN_POINT('Ctrl Pts',(-21.2903253208441,19.2098059207881,
16.9667098902285));
#135996=CARTESIAN_POINT('Ctrl Pts',(-21.2882103114883,19.7131225250721,
16.9916592919231));
#135997=CARTESIAN_POINT('Ctrl Pts',(-20.9008595718265,21.0746360886269,
17.0590006291781));
#135998=CARTESIAN_POINT('Ctrl Pts',(-18.685881688709,22.2377104703834,17.1687339019936));
#135999=CARTESIAN_POINT('Ctrl Pts',(-16.1629699524582,20.8088410866063,
17.2959097086751));
#136000=CARTESIAN_POINT('Ctrl Pts',(-16.0276177675682,18.4219199634484,
17.4007735093137));
#136001=CARTESIAN_POINT('Ctrl Pts',(-16.8552506581505,17.430604537599,17.4632453743918));
#136002=CARTESIAN_POINT('Ctrl Pts',(-17.1769969530062,17.1841723796816,
17.4833253039094));
#136003=CARTESIAN_POINT('Origin',(-18.734,19.211,-1.76670989022852));
#136004=CARTESIAN_POINT('',(-17.174464231106,17.180864983421,18.3499540467144));
#136005=CARTESIAN_POINT('',(-17.174464231106,17.180864983421,18.2832318539276));
#136006=CARTESIAN_POINT('',(-17.174464231106,17.180864983421,-1.76670989022852));
#136007=CARTESIAN_POINT('',(-21.2939989159607,19.2086440968075,17.8332901097715));
#136008=CARTESIAN_POINT('Ctrl Pts',(-21.2939989159607,19.2086440968075,
17.8332901097715));
#136009=CARTESIAN_POINT('Ctrl Pts',(-21.2940751741219,19.2915086264566,
17.837412174938));
#136010=CARTESIAN_POINT('Ctrl Pts',(-21.290123839502,19.3744847533444,17.8415342401044));
#136011=CARTESIAN_POINT('Ctrl Pts',(-21.2821391268744,19.457144246514,17.8456563052709));
#136012=CARTESIAN_POINT('Ctrl Pts',(-21.2741597741335,19.5397482529613,
17.8497756034244));
#136013=CARTESIAN_POINT('Ctrl Pts',(-21.262152459652,19.6220355783688,17.8538949015779));
#136014=CARTESIAN_POINT('Ctrl Pts',(-21.2461634417033,19.7035797825424,
17.8580141997315));
#136015=CARTESIAN_POINT('Ctrl Pts',(-21.2301800733889,19.7850951735057,
17.862132042353));
#136016=CARTESIAN_POINT('Ctrl Pts',(-21.2102178848107,19.8658675009386,
17.8662498849744));
#136017=CARTESIAN_POINT('Ctrl Pts',(-21.1863745538874,19.9454787590158,
17.8703677275959));
#136018=CARTESIAN_POINT('Ctrl Pts',(-21.1625320679642,20.0250871956953,
17.8744854242823));
#136019=CARTESIAN_POINT('Ctrl Pts',(-21.1348088500427,20.1035341923717,
17.8786031209688));
#136020=CARTESIAN_POINT('Ctrl Pts',(-21.1033525053491,20.1804166830605,
17.8827208176552));
#136021=CARTESIAN_POINT('Ctrl Pts',(-21.0718661219911,20.2573725912857,
17.8868424464612));
#136022=CARTESIAN_POINT('Ctrl Pts',(-21.0366396717685,20.3327605713694,
17.8909640752672));
#136023=CARTESIAN_POINT('Ctrl Pts',(-20.9978687619912,20.4061979871471,
17.8950857040732));
#136024=CARTESIAN_POINT('Ctrl Pts',(-20.9590794967267,20.4796701707327,
17.8992092842006));
#136025=CARTESIAN_POINT('Ctrl Pts',(-20.9167426732501,20.551189545137,17.9033328643279));
#136026=CARTESIAN_POINT('Ctrl Pts',(-20.8710983794445,20.6204007650685,
17.9074564444553));
#136027=CARTESIAN_POINT('Ctrl Pts',(-20.8253741239694,20.6897332322411,
17.9115872484506));
#136028=CARTESIAN_POINT('Ctrl Pts',(-20.7763311058832,20.7567490876314,
17.9157180524459));
#136029=CARTESIAN_POINT('Ctrl Pts',(-20.7242507920073,20.8211247730888,
17.9198488564413));
#136030=CARTESIAN_POINT('Ctrl Pts',(-20.6800170723896,20.8758014024867,
17.9233572996922));
#136031=CARTESIAN_POINT('Ctrl Pts',(-20.6335931281538,20.9285739549631,
17.9268657429431));
#136032=CARTESIAN_POINT('Ctrl Pts',(-20.5851713910723,20.9792659530951,
17.9303741861941));
#136033=CARTESIAN_POINT('Ctrl Pts',(-20.5274172101246,21.0397279482481,
17.9345588205871));
#136034=CARTESIAN_POINT('Ctrl Pts',(-20.4665902688467,21.0974699797564,
17.9387434549801));
#136035=CARTESIAN_POINT('Ctrl Pts',(-20.4029770272298,21.1521634868241,
17.9429280893731));
#136036=CARTESIAN_POINT('Ctrl Pts',(-20.3394543311886,21.2067791444542,
17.947106767457));
#136037=CARTESIAN_POINT('Ctrl Pts',(-20.2731535582846,21.2583545993042,
17.9512854455408));
#136038=CARTESIAN_POINT('Ctrl Pts',(-20.2043989371767,21.3065970427421,
17.9554641236247));
#136039=CARTESIAN_POINT('Ctrl Pts',(-20.1344119388974,21.3557041973082,
17.9597177015102));
#136040=CARTESIAN_POINT('Ctrl Pts',(-20.0618825897101,21.4013573280785,
17.9639712793956));
#136041=CARTESIAN_POINT('Ctrl Pts',(-19.9871893049689,21.4432895345164,
17.9682248572811));
#136042=CARTESIAN_POINT('Ctrl Pts',(-19.9139440953056,21.4844088033079,
17.972395971259));
#136043=CARTESIAN_POINT('Ctrl Pts',(-19.8386185251855,21.5219498994727,
17.9765670852369));
#136044=CARTESIAN_POINT('Ctrl Pts',(-19.7615983036838,21.555705040355,17.9807381992148));
#136045=CARTESIAN_POINT('Ctrl Pts',(-19.6846039270611,21.5894488543738,
17.9849079135351));
#136046=CARTESIAN_POINT('Ctrl Pts',(-19.6059164494116,21.619409051666,17.9890776278554));
#136047=CARTESIAN_POINT('Ctrl Pts',(-19.5259437923521,21.6454249895519,
17.9932473421757));
#136048=CARTESIAN_POINT('Ctrl Pts',(-19.4459739810632,21.6714400016791,
17.9974169081197));
#136049=CARTESIAN_POINT('Ctrl Pts',(-19.3647195190224,21.6935108919569,
18.0015864740637));
#136050=CARTESIAN_POINT('Ctrl Pts',(-19.2826045027058,21.7115265644681,
18.0057560400077));
#136051=CARTESIAN_POINT('Ctrl Pts',(-19.1976024237129,21.7301756458007,
18.0100722027467));
#136052=CARTESIAN_POINT('Ctrl Pts',(-19.1116786655147,21.7444789277004,
18.0143883654857));
#136053=CARTESIAN_POINT('Ctrl Pts',(-19.0253143284886,21.7543709839536,
18.0187045282247));
#136054=CARTESIAN_POINT('Ctrl Pts',(-18.9417633006594,21.7639408075146,
18.0228800924163));
#136055=CARTESIAN_POINT('Ctrl Pts',(-18.857800430025,21.7693824000208,18.0270556566079));
#136056=CARTESIAN_POINT('Ctrl Pts',(-18.7738638919265,21.7706896042529,
18.0312312207996));
#136057=CARTESIAN_POINT('Ctrl Pts',(-18.6856879188254,21.7720628322632,
18.0356176828122));
#136058=CARTESIAN_POINT('Ctrl Pts',(-18.5975415917828,21.7688730610124,
18.0400041448249));
#136059=CARTESIAN_POINT('Ctrl Pts',(-18.5099274935594,21.7611748002553,
18.0443906068375));
#136060=CARTESIAN_POINT('Ctrl Pts',(-18.4223133953359,21.7534765394983,
18.0487770688502));
#136061=CARTESIAN_POINT('Ctrl Pts',(-18.3352320899719,21.7412699451077,
18.0531635308629));
#136062=CARTESIAN_POINT('Ctrl Pts',(-18.2491721313432,21.7246710082613,
18.0575499928755));
#136063=CARTESIAN_POINT('Ctrl Pts',(-18.1670719189868,21.7088358131057,
18.0617346272685));
#136064=CARTESIAN_POINT('Ctrl Pts',(-18.0855955387247,21.6889446480546,
18.0659192616614));
#136065=CARTESIAN_POINT('Ctrl Pts',(-18.0051743135506,21.6650605369003,
18.0701038960543));
#136066=CARTESIAN_POINT('Ctrl Pts',(-17.9248675580363,21.641210421822,18.0742825741382));
#136067=CARTESIAN_POINT('Ctrl Pts',(-17.8456134116221,21.6133787796396,
18.078461252222));
#136068=CARTESIAN_POINT('Ctrl Pts',(-17.767833578853,21.5816797435858,18.0826399303058));
#136069=CARTESIAN_POINT('Ctrl Pts',(-17.6886595984782,21.5494125250913,
18.0868935081913));
#136070=CARTESIAN_POINT('Ctrl Pts',(-17.6110137791776,21.5131379942491,
18.0911470860768));
#136071=CARTESIAN_POINT('Ctrl Pts',(-17.5353253711183,21.473029870288,18.0954006639622));
#136072=CARTESIAN_POINT('Ctrl Pts',(-17.4611043305455,21.4336993205758,
18.0995717779401));
#136073=CARTESIAN_POINT('Ctrl Pts',(-17.3887659072355,21.3906827199664,
18.1037428919179));
#136074=CARTESIAN_POINT('Ctrl Pts',(-17.3186935905263,21.3441919199413,
18.1079140058957));
#136075=CARTESIAN_POINT('Ctrl Pts',(-17.2486447872598,21.2977167203531,
18.112083720216));
#136076=CARTESIAN_POINT('Ctrl Pts',(-17.1808609634163,21.2477698907684,
18.1162534345363));
#136077=CARTESIAN_POINT('Ctrl Pts',(-17.1156979943015,21.1946074758762,
18.1204231488565));
#136078=CARTESIAN_POINT('Ctrl Pts',(-17.0505373439648,21.1414469527309,
18.1245927148005));
#136079=CARTESIAN_POINT('Ctrl Pts',(-16.9879977188458,21.0850713632529,
18.1287622807444));
#136080=CARTESIAN_POINT('Ctrl Pts',(-16.9284020884085,21.0257771713509,
18.1329318466883));
#136081=CARTESIAN_POINT('Ctrl Pts',(-16.8667111491206,20.9643982688052,
18.1372480094274));
#136082=CARTESIAN_POINT('Ctrl Pts',(-16.8081754519453,20.8998920810984,
18.1415641721664));
#136083=CARTESIAN_POINT('Ctrl Pts',(-16.7531104204839,20.8326277235434,
18.1458803349055));
#136084=CARTESIAN_POINT('Ctrl Pts',(-16.6998391266337,20.7675544953646,
18.1500558990971));
#136085=CARTESIAN_POINT('Ctrl Pts',(-16.6498160990945,20.6999004393904,
18.1542314632886));
#136086=CARTESIAN_POINT('Ctrl Pts',(-16.6032836911149,20.6300306589538,
18.1584070274802));
#136087=CARTESIAN_POINT('Ctrl Pts',(-16.5544010418242,20.5566319220006,
18.162793489493));
#136088=CARTESIAN_POINT('Ctrl Pts',(-16.5093711996513,20.4807882477349,
18.1671799515058));
#136089=CARTESIAN_POINT('Ctrl Pts',(-16.4684203690348,20.4029517338195,
18.1715664135186));
#136090=CARTESIAN_POINT('Ctrl Pts',(-16.4274695384182,20.3251152199041,
18.1759528755314));
#136091=CARTESIAN_POINT('Ctrl Pts',(-16.3905978935981,20.2452864249786,
18.1803393375442));
#136092=CARTESIAN_POINT('Ctrl Pts',(-16.3579723492966,20.1639389293617,
18.184725799557));
#136093=CARTESIAN_POINT('Ctrl Pts',(-16.3268479546498,20.0863343526005,
18.1889104339505));
#136094=CARTESIAN_POINT('Ctrl Pts',(-16.2994716572956,20.00705890033,18.193095068344));
#136095=CARTESIAN_POINT('Ctrl Pts',(-16.2760239311543,19.926509360513,18.1972797027374));
#136096=CARTESIAN_POINT('Ctrl Pts',(-16.252609579949,19.8460744729961,18.2014583808218));
#136097=CARTESIAN_POINT('Ctrl Pts',(-16.2331128202905,19.7643695380473,
18.2056370589062));
#136098=CARTESIAN_POINT('Ctrl Pts',(-16.2176659448641,19.6818109206073,
18.2098157369906));
#136099=CARTESIAN_POINT('Ctrl Pts',(-16.2019421952991,19.5977724992944,
18.2140693148759));
#136100=CARTESIAN_POINT('Ctrl Pts',(-16.190415125853,19.5128499374393,18.2183228927612));
#136101=CARTESIAN_POINT('Ctrl Pts',(-16.1831710111199,19.4274981974259,
18.2225764706466));
#136102=CARTESIAN_POINT('Ctrl Pts',(-16.1760673376856,19.343801167432,18.2267475846249));
#136103=CARTESIAN_POINT('Ctrl Pts',(-16.1730820747445,19.2596919311863,
18.2309186986033));
#136104=CARTESIAN_POINT('Ctrl Pts',(-16.1742446642318,19.1756076137227,
18.2350898125817));
#136105=CARTESIAN_POINT('Ctrl Pts',(-16.1754068636011,19.0915515115639,
18.2392595269025));
#136106=CARTESIAN_POINT('Ctrl Pts',(-16.180714144804,19.0075207711868,18.2434292412233));
#136107=CARTESIAN_POINT('Ctrl Pts',(-16.1901438433302,18.9239532195391,
18.2475989555441));
#136108=CARTESIAN_POINT('Ctrl Pts',(-16.1995732063072,18.8403886415836,
18.2517685214886));
#136109=CARTESIAN_POINT('Ctrl Pts',(-16.2131246425144,18.757287676623,18.2559380874331));
#136110=CARTESIAN_POINT('Ctrl Pts',(-16.2307236899663,18.6750823611562,
18.2601076533775));
#136111=CARTESIAN_POINT('Ctrl Pts',(-16.2489414982117,18.5899868082277,
18.2644238161159));
#136112=CARTESIAN_POINT('Ctrl Pts',(-16.2714967310844,18.5058515744437,
18.2687399788543));
#136113=CARTESIAN_POINT('Ctrl Pts',(-16.2982497538327,18.4231416762539,
18.2730561415928));
#136114=CARTESIAN_POINT('Ctrl Pts',(-16.3241312996846,18.3431260442806,
18.2772317057848));
#136115=CARTESIAN_POINT('Ctrl Pts',(-16.3539411382345,18.2644447370894,
18.281407269977));
#136116=CARTESIAN_POINT('Ctrl Pts',(-16.3875034565749,18.1874991589187,
18.285582834169));
#136117=CARTESIAN_POINT('Ctrl Pts',(-16.4227609278164,18.1066672425416,
18.2899692961806));
#136118=CARTESIAN_POINT('Ctrl Pts',(-16.4621596558343,18.0277515290341,
18.2943557581922));
#136119=CARTESIAN_POINT('Ctrl Pts',(-16.5054419382126,17.9511869324212,
18.2987422202037));
#136120=CARTESIAN_POINT('Ctrl Pts',(-16.5487242205909,17.8746223358083,
18.3031286822153));
#136121=CARTESIAN_POINT('Ctrl Pts',(-16.5958896819152,17.8004093049793,
18.3075151442268));
#136122=CARTESIAN_POINT('Ctrl Pts',(-16.6466304638567,17.7289445288449,
18.3119016062384));
#136123=CARTESIAN_POINT('Ctrl Pts',(-16.6950307331482,17.6607761980189,
18.3160857345564));
#136124=CARTESIAN_POINT('Ctrl Pts',(-16.7468638869145,17.5948544666272,
18.3202698628743));
#136125=CARTESIAN_POINT('Ctrl Pts',(-16.8018940647046,17.5315457270898,
18.3244539911923));
#136126=CARTESIAN_POINT('Ctrl Pts',(-16.8577907167831,17.467240163678,18.3287040004459));
#136127=CARTESIAN_POINT('Ctrl Pts',(-16.9169857342869,17.4056310236911,
18.3329540096996));
#136128=CARTESIAN_POINT('Ctrl Pts',(-16.9791857557851,17.3470721665525,
18.3372040189533));
#136129=CARTESIAN_POINT('Ctrl Pts',(-17.0413857772832,17.2885133094139,
18.341454028207));
#136130=CARTESIAN_POINT('Ctrl Pts',(-17.1065904878517,17.2330051265689,
18.3457040374607));
#136131=CARTESIAN_POINT('Ctrl Pts',(-17.174464231106,17.180864983421,18.3499540467144));
#136132=CARTESIAN_POINT('Ctrl Pts',(-17.1718943031603,17.177514077948,17.549894074293));
#136133=CARTESIAN_POINT('Ctrl Pts',(-17.8395945142173,16.6654352292226,
17.5919369071391));
#136134=CARTESIAN_POINT('Ctrl Pts',(-19.7363287875448,16.3587000094287,
17.6763716755457));
#136135=CARTESIAN_POINT('Ctrl Pts',(-21.1817726888933,17.9552739588088,
17.7708370080137));
#136136=CARTESIAN_POINT('Ctrl Pts',(-21.2957665006941,19.0070072439541,
17.8232595076358));
#136137=CARTESIAN_POINT('Ctrl Pts',(-21.2939118038754,19.2086434116094,
17.8332900716974));
#136138=CARTESIAN_POINT('',(-21.2939990418858,19.2132148462352,17.7667099127482));
#136139=CARTESIAN_POINT('Ctrl Pts',(-17.1769969530062,17.1841723796816,
17.4833253039094));
#136140=CARTESIAN_POINT('Ctrl Pts',(-17.5345084307618,16.9103469266704,
17.5056373099522));
#136141=CARTESIAN_POINT('Ctrl Pts',(-18.7708037278702,16.3747766682838,
17.5703412515555));
#136142=CARTESIAN_POINT('Ctrl Pts',(-20.7784813956588,17.1540155580924,
17.6648027803286));
#136143=CARTESIAN_POINT('Ctrl Pts',(-21.2874613721703,18.6141143669069,
17.7369523030588));
#136144=CARTESIAN_POINT('Ctrl Pts',(-21.2923873719166,19.2132129984815,
17.7667098902285));
#136145=CARTESIAN_POINT('Ctrl Pts',(-21.2939990418858,19.2132148462352,
17.7667099127482));
#136146=CARTESIAN_POINT('Ctrl Pts',(-21.2939112972768,19.3146332252686,
17.7717442924635));
#136147=CARTESIAN_POINT('Ctrl Pts',(-21.2877929815477,19.415787678657,17.7767786721789));
#136148=CARTESIAN_POINT('Ctrl Pts',(-21.2757605528227,19.5160463769891,
17.7818130518942));
#136149=CARTESIAN_POINT('Ctrl Pts',(-21.2635573150943,19.6177283198494,
17.7869188982603));
#136150=CARTESIAN_POINT('Ctrl Pts',(-21.245270932932,19.7184889031551,17.7920247446265));
#136151=CARTESIAN_POINT('Ctrl Pts',(-21.2210717431444,19.8176911442014,
17.7971305909926));
#136152=CARTESIAN_POINT('Ctrl Pts',(-21.2092508709255,19.866149668042,17.7996247057953));
#136153=CARTESIAN_POINT('Ctrl Pts',(-21.1960198419246,19.9142366801055,
17.8021188205981));
#136154=CARTESIAN_POINT('Ctrl Pts',(-21.1814026084241,19.9618797988219,
17.8046129354008));
#136155=CARTESIAN_POINT('Ctrl Pts',(-21.1568777637899,20.0418155872439,
17.8087975697939));
#136156=CARTESIAN_POINT('Ctrl Pts',(-21.1283869296254,20.1206973427815,
17.8129822041869));
#136157=CARTESIAN_POINT('Ctrl Pts',(-21.0960388974778,20.1981029565359,
17.81716683858));
#136158=CARTESIAN_POINT('Ctrl Pts',(-21.0637369087501,20.27539839298,17.8213455166639));
#136159=CARTESIAN_POINT('Ctrl Pts',(-21.0275888032569,20.3512214402681,
17.8255241947478));
#136160=CARTESIAN_POINT('Ctrl Pts',(-20.987753160177,20.4251650188472,17.8297028728318));
#136161=CARTESIAN_POINT('Ctrl Pts',(-20.9472034918241,20.5004339829302,
17.8339564507172));
#136162=CARTESIAN_POINT('Ctrl Pts',(-20.9028329287838,20.5737549756817,
17.8382100286026));
#136163=CARTESIAN_POINT('Ctrl Pts',(-20.8548601014716,20.6447197878197,
17.8424636064881));
#136164=CARTESIAN_POINT('Ctrl Pts',(-20.8078173210282,20.7143088085979,
17.846634720466));
#136165=CARTESIAN_POINT('Ctrl Pts',(-20.7573109732373,20.7816317931437,
17.850805834444));
#136166=CARTESIAN_POINT('Ctrl Pts',(-20.7035927080245,20.8463301087232,
17.8549769484219));
#136167=CARTESIAN_POINT('Ctrl Pts',(-20.6498924684944,20.9110067141581,
17.8591466627423));
#136168=CARTESIAN_POINT('Ctrl Pts',(-20.592982745675,20.9730600461347,17.8633163770627));
#136169=CARTESIAN_POINT('Ctrl Pts',(-20.533156175962,21.032163653958,17.867486091383));
#136170=CARTESIAN_POINT('Ctrl Pts',(-20.4733317351351,21.0912651586214,
17.8716556573271));
#136171=CARTESIAN_POINT('Ctrl Pts',(-20.4105909816463,21.147416825124,17.8758252232711));
#136172=CARTESIAN_POINT('Ctrl Pts',(-20.3452632200691,21.2003292426475,
17.8799947892152));
#136173=CARTESIAN_POINT('Ctrl Pts',(-20.2776386149852,21.2551019954968,
17.8843109519541));
#136174=CARTESIAN_POINT('Ctrl Pts',(-20.2072421084912,21.3064031452814,
17.888627114693));
#136175=CARTESIAN_POINT('Ctrl Pts',(-20.134474432863,21.3539585537049,17.8929432774319));
#136176=CARTESIAN_POINT('Ctrl Pts',(-20.0640771566148,21.3999648497008,
17.8971188416236));
#136177=CARTESIAN_POINT('Ctrl Pts',(-19.9914612509379,21.4424654946023,
17.9012944058153));
#136178=CARTESIAN_POINT('Ctrl Pts',(-19.9170156443953,21.4812585723032,
17.905469970007));
#136179=CARTESIAN_POINT('Ctrl Pts',(-19.8388099672435,21.522010996137,17.9098564320195));
#136180=CARTESIAN_POINT('Ctrl Pts',(-19.7585854263164,21.558671228602,17.9142428940321));
#136181=CARTESIAN_POINT('Ctrl Pts',(-19.6768157184724,21.5910627136698,
17.9186293560446));
#136182=CARTESIAN_POINT('Ctrl Pts',(-19.5950460106283,21.6234541987376,
17.9230158180572));
#136183=CARTESIAN_POINT('Ctrl Pts',(-19.5117317099373,21.6515768229132,
17.9274022800697));
#136184=CARTESIAN_POINT('Ctrl Pts',(-19.427361531773,21.6753152773656,17.9317887420823));
#136185=CARTESIAN_POINT('Ctrl Pts',(-19.3468733505733,21.6979614903395,
17.9359733764753));
#136186=CARTESIAN_POINT('Ctrl Pts',(-19.2651247293132,21.716702405741,17.9401580108683));
#136187=CARTESIAN_POINT('Ctrl Pts',(-19.1825294815775,21.7314010205036,
17.9443426452614));
#136188=CARTESIAN_POINT('Ctrl Pts',(-19.1000517979537,21.7460787136074,
17.9485213233453));
#136189=CARTESIAN_POINT('Ctrl Pts',(-19.0167303305417,21.7567254548486,
17.9527000014292));
#136190=CARTESIAN_POINT('Ctrl Pts',(-18.9329932047255,21.7632542397796,
17.9568786795131));
#136191=CARTESIAN_POINT('Ctrl Pts',(-18.8477551511093,21.7699000484884,
17.9611322573986));
#136192=CARTESIAN_POINT('Ctrl Pts',(-18.7620868552843,21.7722786894991,
17.965385835284));
#136193=CARTESIAN_POINT('Ctrl Pts',(-18.6764498971537,21.7703530404503,
17.9696394131695));
#136194=CARTESIAN_POINT('Ctrl Pts',(-18.5924731785638,21.768464723866,17.9738105271474));
#136195=CARTESIAN_POINT('Ctrl Pts',(-18.5085270745239,21.76243753283,17.9779816411253));
#136196=CARTESIAN_POINT('Ctrl Pts',(-18.42504935174,21.7522889440085,17.9821527551033));
#136197=CARTESIAN_POINT('Ctrl Pts',(-18.3415996407122,21.742143760644,17.9863224694236));
#136198=CARTESIAN_POINT('Ctrl Pts',(-18.258618455089,21.7278799815763,17.990492183744));
#136199=CARTESIAN_POINT('Ctrl Pts',(-18.1765386867735,21.7095669661339,
17.9946618980643));
#136200=CARTESIAN_POINT('Ctrl Pts',(-18.0944618392085,21.6912546023473,
17.9988314640083));
#136201=CARTESIAN_POINT('Ctrl Pts',(-18.013286793983,21.6688933896802,18.0030010299524));
#136202=CARTESIAN_POINT('Ctrl Pts',(-17.9334351461148,21.6426035685785,
18.0071705958964));
#136203=CARTESIAN_POINT('Ctrl Pts',(-17.8507760128143,21.6153894297986,
18.0114867586353));
#136204=CARTESIAN_POINT('Ctrl Pts',(-17.7695355706381,21.5839654477009,
18.0158029213743));
#136205=CARTESIAN_POINT('Ctrl Pts',(-17.6901612352907,21.5485201888519,
18.0201190841132));
#136206=CARTESIAN_POINT('Ctrl Pts',(-17.6133725105693,21.514229555582,18.0242946483049));
#136207=CARTESIAN_POINT('Ctrl Pts',(-17.5383305816069,21.4761758636208,
18.0284702124965));
#136208=CARTESIAN_POINT('Ctrl Pts',(-17.4654157475494,21.434576846982,18.0326457766882));
#136209=CARTESIAN_POINT('Ctrl Pts',(-17.388818158561,21.3908767629043,18.0370322387008));
#136210=CARTESIAN_POINT('Ctrl Pts',(-17.3145686822397,21.34326410831,18.0414187007134));
#136211=CARTESIAN_POINT('Ctrl Pts',(-17.2430721773898,21.2920416208636,
18.045805162726));
#136212=CARTESIAN_POINT('Ctrl Pts',(-17.1715756725399,21.2408191334172,
18.0501916247386));
#136213=CARTESIAN_POINT('Ctrl Pts',(-17.102832545326,21.185987234388,18.0545780867511));
#136214=CARTESIAN_POINT('Ctrl Pts',(-17.0372042845896,21.1278944415811,
18.0589645487637));
#136215=CARTESIAN_POINT('Ctrl Pts',(-16.9745956774138,21.0724745842853,
18.0631491831568));
#136216=CARTESIAN_POINT('Ctrl Pts',(-16.9145885551714,21.0138810328614,
18.06733381755));
#136217=CARTESIAN_POINT('Ctrl Pts',(-16.8575221052049,20.9523875818855,
18.0715184519431));
#136218=CARTESIAN_POINT('Ctrl Pts',(-16.8005368822664,20.8909816592257,
18.0756971300271));
#136219=CARTESIAN_POINT('Ctrl Pts',(-16.7464843277716,20.8266843701415,
18.0798758081111));
#136220=CARTESIAN_POINT('Ctrl Pts',(-16.6956693348425,20.759808606471,18.0840544861951));
#136221=CARTESIAN_POINT('Ctrl Pts',(-16.6439435196863,20.6917341428008,
18.0883080640805));
#136222=CARTESIAN_POINT('Ctrl Pts',(-16.5955728353227,20.6209881765788,
18.0925616419659));
#136223=CARTESIAN_POINT('Ctrl Pts',(-16.55083834023,20.5479387298265,18.0968152198513));
#136224=CARTESIAN_POINT('Ctrl Pts',(-16.506971110616,20.4763054891424,18.1009863338293));
#136225=CARTESIAN_POINT('Ctrl Pts',(-16.4666005905002,20.4024576962094,
18.1051574478073));
#136226=CARTESIAN_POINT('Ctrl Pts',(-16.4299490395872,20.3267729033368,
18.1093285617853));
#136227=CARTESIAN_POINT('Ctrl Pts',(-16.393309787456,20.2511135072275,18.1134982761058));
#136228=CARTESIAN_POINT('Ctrl Pts',(-16.3603872264447,20.1736187490988,
18.1176679904262));
#136229=CARTESIAN_POINT('Ctrl Pts',(-16.3313573525109,20.0946901654238,
18.1218377047466));
#136230=CARTESIAN_POINT('Ctrl Pts',(-16.3023285115847,20.0157643903665,
18.1260072706907));
#136231=CARTESIAN_POINT('Ctrl Pts',(-16.2771922403253,19.9354053232569,
18.1301768366348));
#136232=CARTESIAN_POINT('Ctrl Pts',(-16.2560756369329,19.854032542659,18.1343464025789));
#136233=CARTESIAN_POINT('Ctrl Pts',(-16.2342165998161,19.7697987954821,
18.1386625653178));
#136234=CARTESIAN_POINT('Ctrl Pts',(-16.2166652853052,19.6844792346862,
18.1429787280566));
#136235=CARTESIAN_POINT('Ctrl Pts',(-16.203505316394,19.5985521335794,18.1472948907955));
#136236=CARTESIAN_POINT('Ctrl Pts',(-16.1907740320855,19.5154240987507,
18.1514704549872));
#136237=CARTESIAN_POINT('Ctrl Pts',(-16.1821523920334,19.4317279704213,
18.1556460191789));
#136238=CARTESIAN_POINT('Ctrl Pts',(-16.177663165104,19.3479013752812,18.1598215833707));
#136239=CARTESIAN_POINT('Ctrl Pts',(-16.1729471979947,19.2598408981034,
18.1642080453831));
#136240=CARTESIAN_POINT('Ctrl Pts',(-16.172792072363,19.1716370118691,18.1685945073955));
#136241=CARTESIAN_POINT('Ctrl Pts',(-16.1771623761343,19.0837940049179,
18.1729809694079));
#136242=CARTESIAN_POINT('Ctrl Pts',(-16.1815326799056,18.9959509979667,
18.1773674314203));
#136243=CARTESIAN_POINT('Ctrl Pts',(-16.1904282787084,18.9084694398441,
18.1817538934327));
#136244=CARTESIAN_POINT('Ctrl Pts',(-16.2037517912763,18.8218419315364,
18.1861403554451));
#136245=CARTESIAN_POINT('Ctrl Pts',(-16.2164587426285,18.7392232130701,
18.1903238287683));
#136246=CARTESIAN_POINT('Ctrl Pts',(-16.2332401386069,18.6570738106168,
18.1945073020916));
#136247=CARTESIAN_POINT('Ctrl Pts',(-16.2540494029882,18.5758267666371,
18.1986907754148));
#136248=CARTESIAN_POINT('Ctrl Pts',(-16.2748315365047,18.494685651561,18.2028687943767));
#136249=CARTESIAN_POINT('Ctrl Pts',(-16.2996310005467,18.4144450007917,
18.2070468133385));
#136250=CARTESIAN_POINT('Ctrl Pts',(-16.3283498001328,18.3355303455408,
18.2112248323003));
#136251=CARTESIAN_POINT('Ctrl Pts',(-16.3570397744324,18.2566948975543,
18.2153986577514));
#136252=CARTESIAN_POINT('Ctrl Pts',(-16.3896411161687,18.1791832320051,
18.2195724832026));
#136253=CARTESIAN_POINT('Ctrl Pts',(-16.4260056863206,18.1034070025396,
18.2237463086537));
#136254=CARTESIAN_POINT('Ctrl Pts',(-16.462344667467,18.0276840952595,18.2279171970691));
#136255=CARTESIAN_POINT('Ctrl Pts',(-16.5024414177568,17.953694611493,18.2320880854844));
#136256=CARTESIAN_POINT('Ctrl Pts',(-16.5460997340485,17.8818301740374,
18.2362589738998));
#136257=CARTESIAN_POINT('Ctrl Pts',(-16.5897512956067,17.809976855314,18.2404292170031));
#136258=CARTESIAN_POINT('Ctrl Pts',(-16.6369631004847,17.7402483290546,
18.2445994601063));
#136259=CARTESIAN_POINT('Ctrl Pts',(-16.6874935461503,17.6730106195583,
18.2487697032096));
#136260=CARTESIAN_POINT('Ctrl Pts',(-16.7380175638304,17.6057814633809,
18.2529394158156));
#136261=CARTESIAN_POINT('Ctrl Pts',(-16.7918591019478,17.5410428584573,
18.2571091284217));
#136262=CARTESIAN_POINT('Ctrl Pts',(-16.8487348978804,17.4791294809571,
18.2612788410277));
#136263=CARTESIAN_POINT('Ctrl Pts',(-16.9056490538859,17.4171743457701,
18.2654513659105));
#136264=CARTESIAN_POINT('Ctrl Pts',(-16.9656012405693,17.3580485804858,
18.2696238907933));
#136265=CARTESIAN_POINT('Ctrl Pts',(-17.0282702918587,17.302051031912,18.2737964156761));
#136266=CARTESIAN_POINT('Ctrl Pts',(-17.0755086731215,17.259841464432,18.2769415617599));
#136267=CARTESIAN_POINT('Ctrl Pts',(-17.1242899094492,17.2194085525259,
18.2800867078438));
#136268=CARTESIAN_POINT('Ctrl Pts',(-17.174464231106,17.180864983421,18.2832318539276));
#136269=CARTESIAN_POINT('Origin',(-18.734,19.211,-1.76670989022852));
#136270=CARTESIAN_POINT('',(-17.1767158295569,17.1837658568561,19.1498287197874));
#136271=CARTESIAN_POINT('',(-17.174464231106,17.180864983421,19.083343695997));
#136272=CARTESIAN_POINT('',(-17.174464231106,17.180864983421,-1.76670989022852));
#136273=CARTESIAN_POINT('',(-21.2936055415609,19.2113823947434,18.6332901348857));
#136274=CARTESIAN_POINT('Ctrl Pts',(-21.2898372017813,19.2113866752102,
18.6332903748237));
#136275=CARTESIAN_POINT('Ctrl Pts',(-21.2903732285223,19.6159817978459,
18.6533365919766));
#136276=CARTESIAN_POINT('Ctrl Pts',(-21.0089154443045,20.8754716727687,
18.7157747446901));
#136277=CARTESIAN_POINT('Ctrl Pts',(-19.0350903746839,22.2230817299851,
18.8206048329641));
#136278=CARTESIAN_POINT('Ctrl Pts',(-16.3642904476992,21.0945520673855,
18.9477806396456));
#136279=CARTESIAN_POINT('Ctrl Pts',(-15.9356497533123,18.6295872620917,
19.0575219352533));
#136280=CARTESIAN_POINT('Ctrl Pts',(-16.7788810677115,17.4923455496799,
19.1248712953006));
#136281=CARTESIAN_POINT('Ctrl Pts',(-17.1767158295569,17.1837658568561,
19.1498287197874));
#136282=CARTESIAN_POINT('Ctrl Pts',(-17.174464231106,17.180864983421,18.3499540467144));
#136283=CARTESIAN_POINT('Ctrl Pts',(-17.2410774775475,17.1296931452628,
18.3541251281992));
#136284=CARTESIAN_POINT('Ctrl Pts',(-17.3102610867351,17.0817656086938,
18.358296209684));
#136285=CARTESIAN_POINT('Ctrl Pts',(-17.3816629355787,17.0373430665829,
18.3624672911689));
#136286=CARTESIAN_POINT('Ctrl Pts',(-17.4530411701186,16.992935216072,18.366636993177));
#136287=CARTESIAN_POINT('Ctrl Pts',(-17.5266357970195,16.9520303006554,
18.3708066951852));
#136288=CARTESIAN_POINT('Ctrl Pts',(-17.6020659860245,16.9148455217461,
18.3749763971933));
#136289=CARTESIAN_POINT('Ctrl Pts',(-17.6774938556494,16.8776618862204,
18.3791459709886));
#136290=CARTESIAN_POINT('Ctrl Pts',(-17.7547567621351,16.8441983623599,
18.3833155447838));
#136291=CARTESIAN_POINT('Ctrl Pts',(-17.8334508010709,16.8146254173631,
18.3874851185791));
#136292=CARTESIAN_POINT('Ctrl Pts',(-17.9145943067586,16.7841319713156,
18.3917844764408));
#136293=CARTESIAN_POINT('Ctrl Pts',(-17.9972590302591,16.7577755082822,
18.3960838343025));
#136294=CARTESIAN_POINT('Ctrl Pts',(-18.0809836050741,16.7356879816965,
18.4003831921643));
#136295=CARTESIAN_POINT('Ctrl Pts',(-18.1622980297666,16.7142362810318,
18.4045587859113));
#136296=CARTESIAN_POINT('Ctrl Pts',(-18.2446116391388,16.6968111018946,
18.4087343796584));
#136297=CARTESIAN_POINT('Ctrl Pts',(-18.3274916636507,16.6834812616959,
18.4129099734055));
#136298=CARTESIAN_POINT('Ctrl Pts',(-18.4140565196421,16.6695587791195,
18.4172712133245));
#136299=CARTESIAN_POINT('Ctrl Pts',(-18.5012387641433,16.6601043283044,
18.4216324532436));
#136300=CARTESIAN_POINT('Ctrl Pts',(-18.5885418813438,16.6551357751796,
18.4259936931626));
#136301=CARTESIAN_POINT('Ctrl Pts',(-18.6758449985444,16.6501672220548,
18.4303549330817));
#136302=CARTESIAN_POINT('Ctrl Pts',(-18.7632684243732,16.6496844955093,
18.4347161730007));
#136303=CARTESIAN_POINT('Ctrl Pts',(-18.8503205710793,16.6536440363642,
18.4390774129198));
#136304=CARTESIAN_POINT('Ctrl Pts',(-18.933847598669,16.6574432382305,18.4432620473123));
#136305=CARTESIAN_POINT('Ctrl Pts',(-19.0173437395032,16.6653459878635,
18.4474466817047));
#136306=CARTESIAN_POINT('Ctrl Pts',(-19.1003730904697,16.6773522820685,
18.4516313160972));
#136307=CARTESIAN_POINT('Ctrl Pts',(-19.1832842594319,16.6893414867997,
18.4558099941806));
#136308=CARTESIAN_POINT('Ctrl Pts',(-19.2657295068657,16.7054225689875,
18.4599886722639));
#136309=CARTESIAN_POINT('Ctrl Pts',(-19.3472750579147,16.7255435623734,
18.4641673503473));
#136310=CARTESIAN_POINT('Ctrl Pts',(-19.4302822543748,16.7460252101085,
18.4684209282329));
#136311=CARTESIAN_POINT('Ctrl Pts',(-19.5123567014431,16.7706930025013,
18.4726745061185));
#136312=CARTESIAN_POINT('Ctrl Pts',(-19.5930485432792,16.7994371042227,
18.476928084004));
#136313=CARTESIAN_POINT('Ctrl Pts',(-19.6721760162898,16.8276239454376,
18.4810991979814));
#136314=CARTESIAN_POINT('Ctrl Pts',(-19.7499735613558,16.8597302905281,
18.4852703119587));
#136315=CARTESIAN_POINT('Ctrl Pts',(-19.8260310897316,16.8956019566693,
18.4894414259361));
#136316=CARTESIAN_POINT('Ctrl Pts',(-19.9020630962693,16.9314615857266,
18.4936111402559));
#136317=CARTESIAN_POINT('Ctrl Pts',(-19.976355829979,16.9710838304488,18.4977808545756));
#136318=CARTESIAN_POINT('Ctrl Pts',(-20.0485201368038,17.0142667868088,
18.5019505688954));
#136319=CARTESIAN_POINT('Ctrl Pts',(-20.1206818757128,17.0574482065338,
18.5061201348388));
#136320=CARTESIAN_POINT('Ctrl Pts',(-20.1907149440086,17.1041898490227,
18.5102897007823));
#136321=CARTESIAN_POINT('Ctrl Pts',(-20.25825690416,17.1542450583211,18.5144592667257));
#136322=CARTESIAN_POINT('Ctrl Pts',(-20.3281735563298,17.2060601470446,
18.5187754294653));
#136323=CARTESIAN_POINT('Ctrl Pts',(-20.3954202425942,17.2614258339352,
18.523091592205));
#136324=CARTESIAN_POINT('Ctrl Pts',(-20.4596314884403,17.3200224839773,
18.5274077549446));
#136325=CARTESIAN_POINT('Ctrl Pts',(-20.5217510596875,17.37671035429,18.5315833191357));
#136326=CARTESIAN_POINT('Ctrl Pts',(-20.5810296141605,17.4364215555172,
18.5357588833267));
#136327=CARTESIAN_POINT('Ctrl Pts',(-20.6371745600437,17.4988298583369,
18.5399344475178));
#136328=CARTESIAN_POINT('Ctrl Pts',(-20.6961552536984,17.5643902562004,
18.5443209095317));
#136329=CARTESIAN_POINT('Ctrl Pts',(-20.7516770948093,17.6329269235829,
18.5487073715456));
#136330=CARTESIAN_POINT('Ctrl Pts',(-20.8034508935159,17.7040252160948,
18.5530938335595));
#136331=CARTESIAN_POINT('Ctrl Pts',(-20.8552246922225,17.7751235086066,
18.5574802955734));
#136332=CARTESIAN_POINT('Ctrl Pts',(-20.9032501953502,17.8487828986681,
18.5618667575873));
#136333=CARTESIAN_POINT('Ctrl Pts',(-20.9472937739972,17.9245589131308,
18.5662532196012));
#136334=CARTESIAN_POINT('Ctrl Pts',(-20.9909726387699,17.9997074453438,
18.5706033584188));
#136335=CARTESIAN_POINT('Ctrl Pts',(-21.0308877830075,18.0771985084606,
18.5749534972363));
#136336=CARTESIAN_POINT('Ctrl Pts',(-21.0667913726612,18.1566355413627,
18.5793036360538));
#136337=CARTESIAN_POINT('Ctrl Pts',(-21.1039225287098,18.2387885765656,
18.5838025088636));
#136338=CARTESIAN_POINT('Ctrl Pts',(-21.1367625751612,18.3230227236645,
18.5883013816734));
#136339=CARTESIAN_POINT('Ctrl Pts',(-21.1650869626505,18.4088677290927,
18.5928002544832));
#136340=CARTESIAN_POINT('Ctrl Pts',(-21.1923645588302,18.4915401396792,
18.5971328613513));
#136341=CARTESIAN_POINT('Ctrl Pts',(-21.2154541944225,18.5757060184776,
18.6014654682194));
#136342=CARTESIAN_POINT('Ctrl Pts',(-21.234202937817,18.6609224875245,18.6057980750875));
#136343=CARTESIAN_POINT('Ctrl Pts',(-21.2529274817652,18.7460289656604,
18.6101250897574));
#136344=CARTESIAN_POINT('Ctrl Pts',(-21.2673221897251,18.8321829392873,
18.6144521044274));
#136345=CARTESIAN_POINT('Ctrl Pts',(-21.2772839154183,18.9189265065526,
18.6187791190974));
#136346=CARTESIAN_POINT('Ctrl Pts',(-21.2872318317724,19.0055498264465,
18.6231001354881));
#136347=CARTESIAN_POINT('Ctrl Pts',(-21.2927589555479,19.0927607071587,
18.6274211518788));
#136348=CARTESIAN_POINT('Ctrl Pts',(-21.2938134141941,19.1800923227686,
18.6317421682696));
#136349=CARTESIAN_POINT('Ctrl Pts',(-21.2939393290371,19.1905207513303,
18.6322581487702));
#136350=CARTESIAN_POINT('Ctrl Pts',(-21.2940015277988,19.2009508929668,
18.6327741292709));
#136351=CARTESIAN_POINT('Ctrl Pts',(-21.2939999715072,19.2113819467094,
18.6332901097715));
#136352=CARTESIAN_POINT('',(-21.2939999971965,19.2111198080496,18.5667098901964));
#136353=CARTESIAN_POINT('Ctrl Pts',(-17.174464231106,17.180864983421,18.2832318539276));
#136354=CARTESIAN_POINT('Ctrl Pts',(-17.2411083724626,17.1296694120014,
18.2874094003952));
#136355=CARTESIAN_POINT('Ctrl Pts',(-17.3102109927058,17.0818088780222,
18.2915869468627));
#136356=CARTESIAN_POINT('Ctrl Pts',(-17.3813970185547,17.0375085289826,
18.2957644933303));
#136357=CARTESIAN_POINT('Ctrl Pts',(-17.4526990807105,16.9931359684545,
18.2999488493796));
#136358=CARTESIAN_POINT('Ctrl Pts',(-17.5260909246801,16.9523353976319,
18.3041332054289));
#136359=CARTESIAN_POINT('Ctrl Pts',(-17.6011737540801,16.9152855803574,
18.3083175614783));
#136360=CARTESIAN_POINT('Ctrl Pts',(-17.6310715508009,16.9005324348744,
18.3099837616943));
#136361=CARTESIAN_POINT('Ctrl Pts',(-17.6612372642791,16.8863734711475,
18.3116499619104));
#136362=CARTESIAN_POINT('Ctrl Pts',(-17.6916449845519,16.8728177954295,
18.3133161621265));
#136363=CARTESIAN_POINT('Ctrl Pts',(-17.7680134730662,16.8387729391863,
18.3175007965194));
#136364=CARTESIAN_POINT('Ctrl Pts',(-17.8461937671331,16.8084101229908,
18.3216854309124));
#136365=CARTESIAN_POINT('Ctrl Pts',(-17.9257962079479,16.7819247375776,
18.3258700653053));
#136366=CARTESIAN_POINT('Ctrl Pts',(-18.0052853445408,16.7554770508323,
18.3300487433892));
#136367=CARTESIAN_POINT('Ctrl Pts',(-18.0861921743122,16.7328959763057,
18.334227421473));
#136368=CARTESIAN_POINT('Ctrl Pts',(-18.1681056484765,16.714329500532,18.3384060995568));
#136369=CARTESIAN_POINT('Ctrl Pts',(-18.2514873627979,16.6954302340229,
18.3426596774423));
#136370=CARTESIAN_POINT('Ctrl Pts',(-18.3359117243126,16.6806911015683,
18.3469132553277));
#136371=CARTESIAN_POINT('Ctrl Pts',(-18.4209273694984,16.6702155683666,
18.3511668332132));
#136372=CARTESIAN_POINT('Ctrl Pts',(-18.5042948205052,16.6599431238176,
18.355337947191));
#136373=CARTESIAN_POINT('Ctrl Pts',(-18.5882303557915,16.6537704962434,
18.3595090611689));
#136374=CARTESIAN_POINT('Ctrl Pts',(-18.6722982812007,16.6517436826497,
18.3636801751467));
#136375=CARTESIAN_POINT('Ctrl Pts',(-18.7563379968057,16.649717549173,18.367849889467));
#136376=CARTESIAN_POINT('Ctrl Pts',(-18.8405095547889,16.6518344778738,
18.3720196037873));
#136377=CARTESIAN_POINT('Ctrl Pts',(-18.9243745836524,16.6580884234077,
18.3761893181075));
#136378=CARTESIAN_POINT('Ctrl Pts',(-19.0082366282384,16.6643421463994,
18.3803588840514));
#136379=CARTESIAN_POINT('Ctrl Pts',(-19.0917917066962,16.6747325584671,
18.3845284499954));
#136380=CARTESIAN_POINT('Ctrl Pts',(-19.1746052695965,16.6892016344672,
18.3886980159393));
#136381=CARTESIAN_POINT('Ctrl Pts',(-19.2603304552117,16.7041794253309,
18.3930141786784));
#136382=CARTESIAN_POINT('Ctrl Pts',(-19.3452604921649,16.723527937402,18.3973303414174));
#136383=CARTESIAN_POINT('Ctrl Pts',(-19.4289254033766,16.7471252702822,
18.4016465041565));
#136384=CARTESIAN_POINT('Ctrl Pts',(-19.5098649389009,16.7699539225245,
18.405822068348));
#136385=CARTESIAN_POINT('Ctrl Pts',(-19.5896200744158,16.796758641008,18.4099976325396));
#136386=CARTESIAN_POINT('Ctrl Pts',(-19.667783027385,16.8273789609571,18.4141731967312));
#136387=CARTESIAN_POINT('Ctrl Pts',(-19.7498938053008,16.8595458404767,
18.418559658744));
#136388=CARTESIAN_POINT('Ctrl Pts',(-19.8302467994661,16.8959236625789,
18.4229461207568));
#136389=CARTESIAN_POINT('Ctrl Pts',(-19.9083976363224,16.9362714026064,
18.4273325827696));
#136390=CARTESIAN_POINT('Ctrl Pts',(-19.9865484731787,16.9766191426339,
18.4317190447824));
#136391=CARTESIAN_POINT('Ctrl Pts',(-20.0624966899236,17.0209364424643,
18.4361055067951));
#136392=CARTESIAN_POINT('Ctrl Pts',(-20.1358342086536,17.0689307080656,
18.4404919688079));
#136393=CARTESIAN_POINT('Ctrl Pts',(-20.2057039471168,17.1146555545475,
18.4446710160258));
#136394=CARTESIAN_POINT('Ctrl Pts',(-20.2734659150699,17.1638887348098,
18.4488500632436));
#136395=CARTESIAN_POINT('Ctrl Pts',(-20.3387454860834,17.2164093339998,
18.4530291104615));
#136396=CARTESIAN_POINT('Ctrl Pts',(-20.4039320790894,17.2688551278475,
18.4572022054423));
#136397=CARTESIAN_POINT('Ctrl Pts',(-20.4666429412498,17.3245787540421,
18.461375300423));
#136398=CARTESIAN_POINT('Ctrl Pts',(-20.5265316718114,17.3833156165374,
18.4655483954038));
#136399=CARTESIAN_POINT('Ctrl Pts',(-20.5870226816091,17.4426431743496,
18.4697634576868));
#136400=CARTESIAN_POINT('Ctrl Pts',(-20.6446340707896,17.5050446643085,
18.4739785199699));
#136401=CARTESIAN_POINT('Ctrl Pts',(-20.6990425114803,17.5702050926228,
18.4781935822529));
#136402=CARTESIAN_POINT('Ctrl Pts',(-20.7528122887529,17.6346006473008,
18.4823591668069));
#136403=CARTESIAN_POINT('Ctrl Pts',(-20.8034536124378,17.701690347722,18.4865247513609));
#136404=CARTESIAN_POINT('Ctrl Pts',(-20.8506921231952,17.7711338758054,
18.4906903359149));
#136405=CARTESIAN_POINT('Ctrl Pts',(-20.8979149500342,17.84055434756,18.4948545374302));
#136406=CARTESIAN_POINT('Ctrl Pts',(-20.9417369482813,17.9123267137653,
18.4990187389455));
#136407=CARTESIAN_POINT('Ctrl Pts',(-20.9819260328715,17.9860801859964,
18.5031829404608));
#136408=CARTESIAN_POINT('Ctrl Pts',(-21.0221139173364,18.0598314558035,
18.5073470176248));
#136409=CARTESIAN_POINT('Ctrl Pts',(-21.0586688839109,18.1355633083682,
18.5115110947889));
#136410=CARTESIAN_POINT('Ctrl Pts',(-21.0914046022626,18.2128799965779,
18.5156751719529));
#136411=CARTESIAN_POINT('Ctrl Pts',(-21.1248385440613,18.2918457802491,
18.5199280651399));
#136412=CARTESIAN_POINT('Ctrl Pts',(-21.1542882228968,18.3724643312946,
18.5241809583268));
#136413=CARTESIAN_POINT('Ctrl Pts',(-21.1796074785073,18.4542939401135,
18.5284338515138));
#136414=CARTESIAN_POINT('Ctrl Pts',(-21.2044336791702,18.5345300386761,
18.5326039259141));
#136415=CARTESIAN_POINT('Ctrl Pts',(-21.2252888283686,18.6159299801768,
18.5367740003144));
#136416=CARTESIAN_POINT('Ctrl Pts',(-21.2420864983912,18.6980651926534,
18.5409440747148));
#136417=CARTESIAN_POINT('Ctrl Pts',(-21.2593845777047,18.7826472458753,
18.545238377295));
#136418=CARTESIAN_POINT('Ctrl Pts',(-21.2723795196075,18.8680085473307,
18.5495326798753));
#136419=CARTESIAN_POINT('Ctrl Pts',(-21.2810343673868,18.9536754357808,
18.5538269824556));
#136420=CARTESIAN_POINT('Ctrl Pts',(-21.2896892151661,19.0393423242309,
18.5581212850358));
#136421=CARTESIAN_POINT('Ctrl Pts',(-21.2940040128973,19.125314270194,18.5624155876161));
#136422=CARTESIAN_POINT('Ctrl Pts',(-21.2939999971965,19.2111198080496,
18.5667098901964));
#136423=CARTESIAN_POINT('Ctrl Pts',(-21.2939999971965,19.2111198086917,
18.5667098902285));
#136424=CARTESIAN_POINT('Ctrl Pts',(-21.2939996986147,19.2174997239769,
18.5670291853155));
#136425=CARTESIAN_POINT('Ctrl Pts',(-21.2939755504833,19.223879573923,18.5673484804024));
#136426=CARTESIAN_POINT('Ctrl Pts',(-21.2939275539577,19.2302592442234,
18.5676677754894));
#136427=CARTESIAN_POINT('Ctrl Pts',(-21.2932985185608,19.31387026376,18.5718524098819));
#136428=CARTESIAN_POINT('Ctrl Pts',(-21.2885677156651,19.3976060296583,
18.5760370442745));
#136429=CARTESIAN_POINT('Ctrl Pts',(-21.2797186185528,19.4810309522135,
18.580221678667));
#136430=CARTESIAN_POINT('Ctrl Pts',(-21.2708821170351,19.5643371297175,
18.5844003567505));
#136431=CARTESIAN_POINT('Ctrl Pts',(-21.2579390129528,19.6473328891638,
18.5885790348339));
#136432=CARTESIAN_POINT('Ctrl Pts',(-21.2409247859828,19.7295827970778,
18.5927577129174));
#136433=CARTESIAN_POINT('Ctrl Pts',(-21.2236055912197,19.8133069754917,
18.5970112908029));
#136434=CARTESIAN_POINT('Ctrl Pts',(-21.2020678918843,19.8962578184688,
18.6012648686885));
#136435=CARTESIAN_POINT('Ctrl Pts',(-21.1764043852928,19.9779816286603,
18.605518446574));
#136436=CARTESIAN_POINT('Ctrl Pts',(-21.1512384158585,20.0581210633086,
18.6096895605515));
#136437=CARTESIAN_POINT('Ctrl Pts',(-21.1221053294156,20.1370801583403,
18.613860674529));
#136438=CARTESIAN_POINT('Ctrl Pts',(-21.0891436468889,20.2144432731942,
18.6180317885065));
#136439=CARTESIAN_POINT('Ctrl Pts',(-21.0561930249731,20.2917804281078,
18.6222015028263));
#136440=CARTESIAN_POINT('Ctrl Pts',(-21.0194165386216,20.3675222435798,
18.6263712171462));
#136441=CARTESIAN_POINT('Ctrl Pts',(-20.9790011895033,20.4412721890413,
18.6305409314661));
#136442=CARTESIAN_POINT('Ctrl Pts',(-20.9385872785366,20.5150195101634,
18.6347104974097));
#136443=CARTESIAN_POINT('Ctrl Pts',(-20.8945349840829,20.5867746991834,
18.6388800633533));
#136444=CARTESIAN_POINT('Ctrl Pts',(-20.8470770406692,20.6561662258013,
18.6430496292968));
#136445=CARTESIAN_POINT('Ctrl Pts',(-20.7979505344985,20.7279974729093,
18.6473657920363));
#136446=CARTESIAN_POINT('Ctrl Pts',(-20.7451747360215,20.7972953169815,
18.6516819547758));
#136447=CARTESIAN_POINT('Ctrl Pts',(-20.6890551911697,20.863682425477,18.6559981175153));
#136448=CARTESIAN_POINT('Ctrl Pts',(-20.634763734602,20.9279069808801,18.6601736817066));
#136449=CARTESIAN_POINT('Ctrl Pts',(-20.5773433873057,20.9894072108732,
18.6643492458978));
#136450=CARTESIAN_POINT('Ctrl Pts',(-20.517109048565,21.0478783631274,18.668524810089));
#136451=CARTESIAN_POINT('Ctrl Pts',(-20.4538324165451,21.1093027543023,
18.6729112721026));
#136452=CARTESIAN_POINT('Ctrl Pts',(-20.3874504923528,21.1673836440657,
18.6772977341163));
#136453=CARTESIAN_POINT('Ctrl Pts',(-20.3183666557521,21.2218163268038,
18.6816841961299));
#136454=CARTESIAN_POINT('Ctrl Pts',(-20.2492828191514,21.276249009542,18.6860706581436));
#136455=CARTESIAN_POINT('Ctrl Pts',(-20.1774975877418,21.327033212256,18.6904571201572));
#136456=CARTESIAN_POINT('Ctrl Pts',(-20.1034462555222,21.3739186191894,
18.6948435821709));
#136457=CARTESIAN_POINT('Ctrl Pts',(-20.032802134896,21.4186467590315,18.6990282165633));
#136458=CARTESIAN_POINT('Ctrl Pts',(-19.9598329133702,21.459993484366,18.7032128509558));
#136459=CARTESIAN_POINT('Ctrl Pts',(-19.8848959073541,21.497709122393,18.7073974853483));
#136460=CARTESIAN_POINT('Ctrl Pts',(-19.8100655648908,21.5353710768775,
18.7115761634316));
#136461=CARTESIAN_POINT('Ctrl Pts',(-19.733273408809,21.5694120050826,18.715754841515));
#136462=CARTESIAN_POINT('Ctrl Pts',(-19.654904774228,21.5996260479204,18.7199335195984));
#136463=CARTESIAN_POINT('Ctrl Pts',(-19.5751314381808,21.630381655767,18.7241870974839));
#136464=CARTESIAN_POINT('Ctrl Pts',(-19.493724958338,21.6571715770569,18.7284406753695));
#136465=CARTESIAN_POINT('Ctrl Pts',(-19.41111699767,21.6798281777933,18.7326942532551));
#136466=CARTESIAN_POINT('Ctrl Pts',(-19.3301105535301,21.7020455361098,
18.7368653672325));
#136467=CARTESIAN_POINT('Ctrl Pts',(-19.2479492630204,21.7202882813848,
18.7410364812098));
#136468=CARTESIAN_POINT('Ctrl Pts',(-19.1650575928257,21.734447909442,18.7452075951871));
#136469=CARTESIAN_POINT('Ctrl Pts',(-19.0821937377315,21.7486027860993,
18.7493773095069));
#136470=CARTESIAN_POINT('Ctrl Pts',(-18.9986004427839,21.7586771892408,
18.7535470238267));
#136471=CARTESIAN_POINT('Ctrl Pts',(-18.9147123478954,21.7646137232005,
18.7577167381465));
#136472=CARTESIAN_POINT('Ctrl Pts',(-18.8308272381054,21.7705500459129,
18.7618863040899));
#136473=CARTESIAN_POINT('Ctrl Pts',(-18.7466478081773,21.7723487605766,
18.7660558700333));
#136474=CARTESIAN_POINT('Ctrl Pts',(-18.6626124310825,21.7700044577929,
18.7702254359768));
#136475=CARTESIAN_POINT('Ctrl Pts',(-18.5756224737711,21.7675777322146,
18.7745415987164));
#136476=CARTESIAN_POINT('Ctrl Pts',(-18.4887874147817,21.7607112463061,
18.778857761456));
#136477=CARTESIAN_POINT('Ctrl Pts',(-18.4025899172848,21.749457672894,18.7831739241957));
#136478=CARTESIAN_POINT('Ctrl Pts',(-18.3192002942283,21.7385706834556,
18.7873494883867));
#136479=CARTESIAN_POINT('Ctrl Pts',(-18.2364077885004,21.7235781663988,
18.7915250525778));
#136480=CARTESIAN_POINT('Ctrl Pts',(-18.1546390975914,21.7045799455322,
18.7957006167689));
#136481=CARTESIAN_POINT('Ctrl Pts',(-18.0687404644519,21.6846221696844,
18.8000870787828));
#136482=CARTESIAN_POINT('Ctrl Pts',(-17.9839723511224,21.6602435606427,
18.8044735407967));
#136483=CARTESIAN_POINT('Ctrl Pts',(-17.9008093086191,21.6316183655827,
18.8088600028106));
#136484=CARTESIAN_POINT('Ctrl Pts',(-17.8176462661158,21.6029931705227,
18.8132464648245));
#136485=CARTESIAN_POINT('Ctrl Pts',(-17.7360888041544,21.5701216768946,
18.8176329268384));
#136486=CARTESIAN_POINT('Ctrl Pts',(-17.6565830150584,21.5332344068933,
18.8220193888523));
#136487=CARTESIAN_POINT('Ctrl Pts',(-17.5807354051426,21.4980443748501,
18.8262040232484));
#136488=CARTESIAN_POINT('Ctrl Pts',(-17.5064724966939,21.4590690053602,
18.8303886576445));
#136489=CARTESIAN_POINT('Ctrl Pts',(-17.4341976336211,21.416473601827,18.8345732920406));
#136490=CARTESIAN_POINT('Ctrl Pts',(-17.3620256448697,21.3739388275783,
18.8387519701277));
#136491=CARTESIAN_POINT('Ctrl Pts',(-17.2918364736816,21.327794485688,18.8429306482147));
#136492=CARTESIAN_POINT('Ctrl Pts',(-17.2240117895636,21.2782531543918,
18.8471093263017));
#136493=CARTESIAN_POINT('Ctrl Pts',(-17.1549713967908,21.2278238303831,
18.8513629041864));
#136494=CARTESIAN_POINT('Ctrl Pts',(-17.0883815290674,21.173874739978,18.855616482071));
#136495=CARTESIAN_POINT('Ctrl Pts',(-17.0246167910337,21.1166781063191,
18.8598700599557));
#136496=CARTESIAN_POINT('Ctrl Pts',(-16.9620882568161,21.0605903409623,
18.8640411739367));
#136497=CARTESIAN_POINT('Ctrl Pts',(-16.9022766467391,21.0013801499079,
18.8682122879177));
#136498=CARTESIAN_POINT('Ctrl Pts',(-16.8455029514096,20.9393457112121,
18.8723834018988));
#136499=CARTESIAN_POINT('Ctrl Pts',(-16.788748307042,20.8773320887715,18.8765531162222));
#136500=CARTESIAN_POINT('Ctrl Pts',(-16.7350298632001,20.8124964399251,
18.8807228305456));
#136501=CARTESIAN_POINT('Ctrl Pts',(-16.6846311428973,20.7451731608712,
18.8848925448691));
#136502=CARTESIAN_POINT('Ctrl Pts',(-16.6342342159975,20.6778522774687,
18.8890621108162));
#136503=CARTESIAN_POINT('Ctrl Pts',(-16.5871570527732,20.6080443086434,
18.8932316767633));
#136504=CARTESIAN_POINT('Ctrl Pts',(-16.5436414846482,20.5361149286858,
18.8974012427104));
#136505=CARTESIAN_POINT('Ctrl Pts',(-16.4985959629012,20.4616566005807,
18.9017174054456));
#136506=CARTESIAN_POINT('Ctrl Pts',(-16.4573674205007,20.384925359397,18.9060335681809));
#136507=CARTESIAN_POINT('Ctrl Pts',(-16.420172824354,20.3063555592783,18.9103497309162));
#136508=CARTESIAN_POINT('Ctrl Pts',(-16.3841898382084,20.2303451620158,
18.9145252951109));
#136509=CARTESIAN_POINT('Ctrl Pts',(-16.3519821593669,20.1526146016957,
18.9187008593055));
#136510=CARTESIAN_POINT('Ctrl Pts',(-16.3236968150629,20.0735766961158,
18.9228764235002));
#136511=CARTESIAN_POINT('Ctrl Pts',(-16.2939828453285,19.990546774011,18.9272628855058));
#136512=CARTESIAN_POINT('Ctrl Pts',(-16.2685980256127,19.9060745270031,
18.9316493475114));
#136513=CARTESIAN_POINT('Ctrl Pts',(-16.24765270708,19.8206532940854,18.936035809517));
#136514=CARTESIAN_POINT('Ctrl Pts',(-16.2267073885473,19.7352320611677,
18.9404222715225));
#136515=CARTESIAN_POINT('Ctrl Pts',(-16.210201605397,19.6488624265218,18.9448087335281));
#136516=CARTESIAN_POINT('Ctrl Pts',(-16.1981829862585,19.5620442604845,
18.9491951955337));
#136517=CARTESIAN_POINT('Ctrl Pts',(-16.1867173615958,19.4792207269146,
18.9533798299225));
#136518=CARTESIAN_POINT('Ctrl Pts',(-16.1792923755172,19.3956807451282,
18.9575644643113));
#136519=CARTESIAN_POINT('Ctrl Pts',(-16.1759873564286,19.3118529391174,
18.9617490987001));
#136520=CARTESIAN_POINT('Ctrl Pts',(-16.1726870416255,19.2281444516125,
18.9659277767798));
#136521=CARTESIAN_POINT('Ctrl Pts',(-16.173495063509,19.1441494093851,18.9701064548596));
#136522=CARTESIAN_POINT('Ctrl Pts',(-16.1784392678899,19.0603038006557,
18.9742851329393));
#136523=CARTESIAN_POINT('Ctrl Pts',(-16.1834720935873,18.974955319541,18.9785387108258));
#136524=CARTESIAN_POINT('Ctrl Pts',(-16.1927909085457,18.8897621593934,
18.9827922887123));
#136525=CARTESIAN_POINT('Ctrl Pts',(-16.2063695825696,18.8051866526586,
18.9870458665988));
#136526=CARTESIAN_POINT('Ctrl Pts',(-16.2196850074843,18.7222508072609,
18.9912169805725));
#136527=CARTESIAN_POINT('Ctrl Pts',(-16.2370965177706,18.6399093552906,
18.9953880945463));
#136528=CARTESIAN_POINT('Ctrl Pts',(-16.2585271389987,18.5585935971758,
18.9995592085201));
#136529=CARTESIAN_POINT('Ctrl Pts',(-16.279950568975,18.4773051253485,19.0037289228363));
#136530=CARTESIAN_POINT('Ctrl Pts',(-16.3053903143098,18.3970421082999,
19.0078986371526));
#136531=CARTESIAN_POINT('Ctrl Pts',(-16.3347186663499,18.3182239463347,
19.0120683514688));
#136532=CARTESIAN_POINT('Ctrl Pts',(-16.3640459747616,18.2394085890572,
19.0162379174088));
#136533=CARTESIAN_POINT('Ctrl Pts',(-16.3972614535261,18.162038415493,19.0204074833487));
#136534=CARTESIAN_POINT('Ctrl Pts',(-16.4341885271975,18.0865147001556,
19.0245770492886));
#136535=CARTESIAN_POINT('Ctrl Pts',(-16.4724139113062,18.008335663989,19.0288932120325));
#136536=CARTESIAN_POINT('Ctrl Pts',(-16.5146165141609,17.9321358186697,
19.0332093747764));
#136537=CARTESIAN_POINT('Ctrl Pts',(-16.5605485527345,17.8583327066941,
19.0375255375203));
#136538=CARTESIAN_POINT('Ctrl Pts',(-16.6049843598895,17.7869337234782,
19.041701101708));
#136539=CARTESIAN_POINT('Ctrl Pts',(-16.6529100541823,17.7177780846056,
19.0458766658957));
#136540=CARTESIAN_POINT('Ctrl Pts',(-16.704058104228,17.6512128671548,19.0500522300834));
#136541=CARTESIAN_POINT('Ctrl Pts',(-16.757789520855,17.5812855985977,19.0544386921054));
#136542=CARTESIAN_POINT('Ctrl Pts',(-16.8150769912952,17.5142177570114,
19.0588251541273));
#136543=CARTESIAN_POINT('Ctrl Pts',(-16.8755654265149,17.450369165306,19.0632116161493));
#136544=CARTESIAN_POINT('Ctrl Pts',(-16.9360538617346,17.3865205736007,
19.0675980781712));
#136545=CARTESIAN_POINT('Ctrl Pts',(-16.9997427890409,17.3258915767388,
19.0719845401932));
#136546=CARTESIAN_POINT('Ctrl Pts',(-17.0662376770542,17.2687927931957,
19.0763710022152));
#136547=CARTESIAN_POINT('Ctrl Pts',(-17.1014709690828,17.2385381649806,
19.0786952334758));
#136548=CARTESIAN_POINT('Ctrl Pts',(-17.1375641351115,17.209211383591,19.0810194647364));
#136549=CARTESIAN_POINT('Ctrl Pts',(-17.174464231106,17.180864983421,19.083343695997));
#136550=CARTESIAN_POINT('Origin',(-18.734,19.211,-1.76670989022852));
#136551=CARTESIAN_POINT('',(-17.174464231106,17.180864983421,19.9498236312054));
#136552=CARTESIAN_POINT('',(-17.174464231106,17.180864983421,19.8833624896767));
#136553=CARTESIAN_POINT('',(-17.174464231106,17.180864983421,-1.76670989022852));
#136554=CARTESIAN_POINT('',(-21.2939990581246,19.2131959965571,19.4332901097715));
#136555=CARTESIAN_POINT('Ctrl Pts',(-21.2939990581246,19.2131959965571,
19.4332901097715));
#136556=CARTESIAN_POINT('Ctrl Pts',(-21.293890587382,19.3396465586196,19.4395926510263));
#136557=CARTESIAN_POINT('Ctrl Pts',(-21.2844099378551,19.465708927393,19.4458951922812));
#136558=CARTESIAN_POINT('Ctrl Pts',(-21.2657470116552,19.5902849443033,
19.452197733536));
#136559=CARTESIAN_POINT('Ctrl Pts',(-21.2615163488398,19.618524841776,19.4536264444811));
#136560=CARTESIAN_POINT('Ctrl Pts',(-21.2568139996567,19.6466884925667,
19.4550551554262));
#136561=CARTESIAN_POINT('Ctrl Pts',(-21.2516424693627,19.6747632978808,
19.4564838663713));
#136562=CARTESIAN_POINT('Ctrl Pts',(-21.2364952751686,19.7569932189831,
19.4606685004935));
#136563=CARTESIAN_POINT('Ctrl Pts',(-21.2172870302474,19.8386332916553,
19.4648531346158));
#136564=CARTESIAN_POINT('Ctrl Pts',(-21.1940771445785,19.9192516803528,
19.469037768738));
#136565=CARTESIAN_POINT('Ctrl Pts',(-21.1709002953099,19.9997553187496,
19.4732164465514));
#136566=CARTESIAN_POINT('Ctrl Pts',(-21.1437332452095,20.0792397234556,
19.4773951243647));
#136567=CARTESIAN_POINT('Ctrl Pts',(-21.1126865924437,20.1572822490824,
19.4815738021781));
#136568=CARTESIAN_POINT('Ctrl Pts',(-21.0810834481907,20.2367236373009,
19.4858273801312));
#136569=CARTESIAN_POINT('Ctrl Pts',(-21.0454603361894,20.3146704722382,
19.4900809580843));
#136570=CARTESIAN_POINT('Ctrl Pts',(-21.0059873753743,20.3906920641166,
19.4943345360374));
#136571=CARTESIAN_POINT('Ctrl Pts',(-20.9672796780334,20.4652398231152,
19.4985056497473));
#136572=CARTESIAN_POINT('Ctrl Pts',(-20.9248702957982,20.5379358953033,
19.5026767634572));
#136573=CARTESIAN_POINT('Ctrl Pts',(-20.8789678616489,20.6083950309391,
19.506847877167));
#136574=CARTESIAN_POINT('Ctrl Pts',(-20.8330808304891,20.6788305233554,
19.5110175912208));
#136575=CARTESIAN_POINT('Ctrl Pts',(-20.7837033261796,20.7470301848417,
19.5151873052746));
#136576=CARTESIAN_POINT('Ctrl Pts',(-20.7310884045781,20.8126360086797,
19.5193570193284));
#136577=CARTESIAN_POINT('Ctrl Pts',(-20.6784753552182,20.8782394980099,
19.5235265850078));
#136578=CARTESIAN_POINT('Ctrl Pts',(-20.6226254060923,20.9412489748611,
19.5276961506871));
#136579=CARTESIAN_POINT('Ctrl Pts',(-20.5638323063888,21.0013389987641,
19.5318657163664));
#136580=CARTESIAN_POINT('Ctrl Pts',(-20.502972105477,21.0635417223146,19.5361818794236));
#136581=CARTESIAN_POINT('Ctrl Pts',(-20.4389583088965,21.122615499409,19.5404980424808));
#136582=CARTESIAN_POINT('Ctrl Pts',(-20.3721573780251,21.1782418267264,
19.544814205538));
#136583=CARTESIAN_POINT('Ctrl Pts',(-20.3075324892011,21.2320561249956,
19.5489897694722));
#136584=CARTESIAN_POINT('Ctrl Pts',(-20.2402996648593,21.2826438810762,
19.5531653334064));
#136585=CARTESIAN_POINT('Ctrl Pts',(-20.1708219662268,21.329759693162,19.5573408973406));
#136586=CARTESIAN_POINT('Ctrl Pts',(-20.0978350996175,21.3792552228008,
19.5617273599593));
#136587=CARTESIAN_POINT('Ctrl Pts',(-20.0223711202591,21.4249185513468,
19.566113822578));
#136588=CARTESIAN_POINT('Ctrl Pts',(-19.9448802161397,21.4665196966911,
19.5705002851967));
#136589=CARTESIAN_POINT('Ctrl Pts',(-19.8673893120203,21.5081208420354,
19.5748867478154));
#136590=CARTESIAN_POINT('Ctrl Pts',(-19.7878720403016,21.5456596252664,
19.579273210434));
#136591=CARTESIAN_POINT('Ctrl Pts',(-19.7068005673304,21.5789651720837,
19.5836596730527));
#136592=CARTESIAN_POINT('Ctrl Pts',(-19.629459322931,21.6107382772446,19.5878443074871));
#136593=CARTESIAN_POINT('Ctrl Pts',(-19.5504158778411,21.6387774071505,
19.5920289419215));
#136594=CARTESIAN_POINT('Ctrl Pts',(-19.4700654949587,21.6628987717953,
19.5962135763559));
#136595=CARTESIAN_POINT('Ctrl Pts',(-19.3898294809474,21.6869858026491,
19.6003922544787));
#136596=CARTESIAN_POINT('Ctrl Pts',(-19.3082906610537,21.7071660136986,
19.6045709326015));
#136597=CARTESIAN_POINT('Ctrl Pts',(-19.2258642779018,21.7233036305598,
19.6087496107243));
#136598=CARTESIAN_POINT('Ctrl Pts',(-19.1419604620487,21.7397305024139,
19.6130031885997));
#136599=CARTESIAN_POINT('Ctrl Pts',(-19.0571373968166,21.7519682444677,
19.6172567664751));
#136600=CARTESIAN_POINT('Ctrl Pts',(-18.9718493062277,21.7599267756307,
19.6215103443505));
#136601=CARTESIAN_POINT('Ctrl Pts',(-18.8882146908505,21.7677310152166,
19.6256814583611));
#136602=CARTESIAN_POINT('Ctrl Pts',(-18.8041333991885,21.7714204401683,
19.6298525723716));
#136603=CARTESIAN_POINT('Ctrl Pts',(-18.7200422944287,21.7709619494155,
19.6340236863821));
#136604=CARTESIAN_POINT('Ctrl Pts',(-18.6359794072993,21.7705036125139,
19.6381934007327));
#136605=CARTESIAN_POINT('Ctrl Pts',(-18.551907173255,21.7659001267009,19.6423631150832));
#136606=CARTESIAN_POINT('Ctrl Pts',(-18.4682635936743,21.7571704896477,
19.6465328294338));
#136607=CARTESIAN_POINT('Ctrl Pts',(-18.3846229905396,21.7484411632376,
19.6507023954056));
#136608=CARTESIAN_POINT('Ctrl Pts',(-18.3014114689995,21.7355860261208,
19.6548719613774));
#136609=CARTESIAN_POINT('Ctrl Pts',(-18.2190616739018,21.7186759201131,
19.6590415273492));
#136610=CARTESIAN_POINT('Ctrl Pts',(-18.1338165629591,21.7011712759185,
19.663357690048));
#136611=CARTESIAN_POINT('Ctrl Pts',(-18.0494954191338,21.679321318249,19.6676738527467));
#136612=CARTESIAN_POINT('Ctrl Pts',(-17.966564411757,21.6532617832448,19.6719900154455));
#136613=CARTESIAN_POINT('Ctrl Pts',(-17.8863348720621,21.6280511344877,
19.6761655796587));
#136614=CARTESIAN_POINT('Ctrl Pts',(-17.8074067178008,21.5989011580654,
19.6803411438719));
#136615=CARTESIAN_POINT('Ctrl Pts',(-17.7301828112741,21.5659842996543,
19.6845167080851));
#136616=CARTESIAN_POINT('Ctrl Pts',(-17.6490585105433,21.5314048897156,
19.6889031700266));
#136617=CARTESIAN_POINT('Ctrl Pts',(-17.5698156696645,21.4926683234483,
19.6932896319682));
#136618=CARTESIAN_POINT('Ctrl Pts',(-17.492891345209,21.4500286525641,19.6976760939097));
#136619=CARTESIAN_POINT('Ctrl Pts',(-17.4159670207535,21.4073889816798,
19.7020625558512));
#136620=CARTESIAN_POINT('Ctrl Pts',(-17.341361664738,21.3608465778214,19.7064490177927));
#136621=CARTESIAN_POINT('Ctrl Pts',(-17.2694745299336,21.3107059669218,
19.7108354797342));
#136622=CARTESIAN_POINT('Ctrl Pts',(-17.2008950125853,21.2628723885714,
19.7150201150467));
#136623=CARTESIAN_POINT('Ctrl Pts',(-17.1345338099885,21.2115863975994,
19.7192047503592));
#136624=CARTESIAN_POINT('Ctrl Pts',(-17.0707594088287,21.1570808657093,
19.7233893856716));
#136625=CARTESIAN_POINT('Ctrl Pts',(-17.0070757825499,21.1026529156246,
19.7275680646793));
#136626=CARTESIAN_POINT('Ctrl Pts',(-16.945971990841,21.0450148234629,19.731746743687));
#136627=CARTESIAN_POINT('Ctrl Pts',(-16.8877869614792,20.9844422506514,
19.7359254226946));
#136628=CARTESIAN_POINT('Ctrl Pts',(-16.8285590235835,20.9227839749746,
19.7401790003497));
#136629=CARTESIAN_POINT('Ctrl Pts',(-16.7723559086582,20.8580852602608,
19.7444325780047));
#136630=CARTESIAN_POINT('Ctrl Pts',(-16.719499223283,20.790679277767,19.7486861556597));
#136631=CARTESIAN_POINT('Ctrl Pts',(-16.6676672535619,20.7245800734972,
19.7528572705652));
#136632=CARTESIAN_POINT('Ctrl Pts',(-16.6190534158838,20.6558780132752,
19.7570283854707));
#136633=CARTESIAN_POINT('Ctrl Pts',(-16.5739220088091,20.5849225130889,
19.7611995003762));
#136634=CARTESIAN_POINT('Ctrl Pts',(-16.528805746017,20.5139908227108,19.7653692156234));
#136635=CARTESIAN_POINT('Ctrl Pts',(-16.4871698397316,20.440807581965,19.7695389308707));
#136636=CARTESIAN_POINT('Ctrl Pts',(-16.4492353977934,20.3657513639325,
19.773708646118));
#136637=CARTESIAN_POINT('Ctrl Pts',(-16.4113023057417,20.2906978167542,
19.7778782129872));
#136638=CARTESIAN_POINT('Ctrl Pts',(-16.3770706229015,20.2137718357625,
19.7820477798563));
#136639=CARTESIAN_POINT('Ctrl Pts',(-16.3467149650018,20.1353755522913,
19.7862173467255));
#136640=CARTESIAN_POINT('Ctrl Pts',(-16.3152920545844,20.054222990857,19.7905335083663));
#136641=CARTESIAN_POINT('Ctrl Pts',(-16.2880229889401,19.9714953049146,
19.7948496700072));
#136642=CARTESIAN_POINT('Ctrl Pts',(-16.2650459639335,19.8876579400192,
19.799165831648));
#136643=CARTESIAN_POINT('Ctrl Pts',(-16.242817402594,19.806551530134,19.8033413967509));
#136644=CARTESIAN_POINT('Ctrl Pts',(-16.224605609274,19.7244070957626,19.8075169618538));
#136645=CARTESIAN_POINT('Ctrl Pts',(-16.2104836462314,19.6416567220678,
19.8116925269566));
#136646=CARTESIAN_POINT('Ctrl Pts',(-16.195648426756,19.5547268843585,19.8160789868665));
#136647=CARTESIAN_POINT('Ctrl Pts',(-16.185327112135,19.4671288674576,19.8204654467763));
#136648=CARTESIAN_POINT('Ctrl Pts',(-16.1795426555597,19.3793676793066,
19.8248519066861));
#136649=CARTESIAN_POINT('Ctrl Pts',(-16.1737581989845,19.2916064911556,
19.829238366596));
#136650=CARTESIAN_POINT('Ctrl Pts',(-16.172510532631,19.20368271299,19.8336248265058));
#136651=CARTESIAN_POINT('Ctrl Pts',(-16.1757597065464,19.1160968865085,
19.8380112864156));
#136652=CARTESIAN_POINT('Ctrl Pts',(-16.1788596427718,19.0325339614677,
19.8421962719934));
#136653=CARTESIAN_POINT('Ctrl Pts',(-16.1860639312761,18.9489675605742,
19.8463812575711));
#136654=CARTESIAN_POINT('Ctrl Pts',(-16.1973762177222,18.8658336818538,
19.8505662431489));
#136655=CARTESIAN_POINT('Ctrl Pts',(-16.2086691571991,18.7828419838145,
19.8547440713065));
#136656=CARTESIAN_POINT('Ctrl Pts',(-16.2240560628308,18.7002817889827,
19.858921899464));
#136657=CARTESIAN_POINT('Ctrl Pts',(-16.2434886327822,18.6185870276919,
19.8630997276216));
#136658=CARTESIAN_POINT('Ctrl Pts',(-16.262902292549,18.5369717650481,19.8672734902592));
#136659=CARTESIAN_POINT('Ctrl Pts',(-16.2863536948447,18.4562207088556,
19.8714472528968));
#136660=CARTESIAN_POINT('Ctrl Pts',(-16.3137431279862,18.3767598226709,
19.8756210155344));
#136661=CARTESIAN_POINT('Ctrl Pts',(-16.3411141250046,18.2973524224668,
19.8797919687673));
#136662=CARTESIAN_POINT('Ctrl Pts',(-16.3724177390461,18.2192339011836,
19.8839629220001));
#136663=CARTESIAN_POINT('Ctrl Pts',(-16.4075041946845,18.1428159017055,
19.888133875233));
#136664=CARTESIAN_POINT('Ctrl Pts',(-16.4425775587027,18.0664264156637,
19.8923032721806));
#136665=CARTESIAN_POINT('Ctrl Pts',(-16.4814307675656,17.991736608042,19.8964726691282));
#136666=CARTESIAN_POINT('Ctrl Pts',(-16.5238661307731,17.9191376698363,
19.9006420660758));
#136667=CARTESIAN_POINT('Ctrl Pts',(-16.566318136594,17.8465102592441,19.9048130982082));
#136668=CARTESIAN_POINT('Ctrl Pts',(-16.6123548789664,17.775975758528,19.9089841303406));
#136669=CARTESIAN_POINT('Ctrl Pts',(-16.6617333188454,17.7078996034276,
19.913155162473));
#136670=CARTESIAN_POINT('Ctrl Pts',(-16.7111193623267,17.6398129655331,
19.9173268368871));
#136671=CARTESIAN_POINT('Ctrl Pts',(-16.7638478477789,17.5741857926268,
19.9214985113013));
#136672=CARTESIAN_POINT('Ctrl Pts',(-16.8196343586719,17.51135174483,19.9256701857154));
#136673=CARTESIAN_POINT('Ctrl Pts',(-16.875489508745,17.4484403866323,19.9298469929171));
#136674=CARTESIAN_POINT('Ctrl Pts',(-16.9344098861507,17.3883293561259,
19.9340238001189));
#136675=CARTESIAN_POINT('Ctrl Pts',(-16.9960732542543,17.3313163493764,
19.9382006073206));
#136676=CARTESIAN_POINT('Ctrl Pts',(-17.0532712339288,17.2784319724516,
19.9420749486156));
#136677=CARTESIAN_POINT('Ctrl Pts',(-17.1128287126708,17.2282129651311,
19.9459492899105));
#136678=CARTESIAN_POINT('Ctrl Pts',(-17.174464231106,17.180864983421,19.9498236312055));
#136679=CARTESIAN_POINT('Ctrl Pts',(-17.1767158295569,17.1837658568561,
19.1498287197874));
#136680=CARTESIAN_POINT('Ctrl Pts',(-17.4546313077574,16.9682013031296,
19.1672632308611));
#136681=CARTESIAN_POINT('Ctrl Pts',(-18.5512406904231,16.4174579447905,
19.2270896774953));
#136682=CARTESIAN_POINT('Ctrl Pts',(-20.635918474416,16.9602241188658,19.3215765970806));
#136683=CARTESIAN_POINT('Ctrl Pts',(-21.2889869220882,18.5174131978834,
19.3986290055925));
#136684=CARTESIAN_POINT('Ctrl Pts',(-21.2953149015357,19.2131844541912,
19.4332894785437));
#136685=CARTESIAN_POINT('',(-21.2939989850552,19.2087204131754,19.3667098901939));
#136686=CARTESIAN_POINT('Ctrl Pts',(-17.174464231106,17.180864983421,19.083343695997));
#136687=CARTESIAN_POINT('Ctrl Pts',(-17.2408453266491,17.1298714819877,
19.0875248509024));
#136688=CARTESIAN_POINT('Ctrl Pts',(-17.3098397832821,17.0820529442478,
19.0917060058077));
#136689=CARTESIAN_POINT('Ctrl Pts',(-17.3811106246903,17.037686783233,19.0958871607131));
#136690=CARTESIAN_POINT('Ctrl Pts',(-17.452293133591,16.9933756092813,19.1000631335287));
#136691=CARTESIAN_POINT('Ctrl Pts',(-17.5257460343461,16.9525085530914,
19.1042391063443));
#136692=CARTESIAN_POINT('Ctrl Pts',(-17.6011010651429,16.9153214503334,
19.1084150791599));
#136693=CARTESIAN_POINT('Ctrl Pts',(-17.6763878065308,16.8781680478504,
19.1125872675604));
#136694=CARTESIAN_POINT('Ctrl Pts',(-17.7535728413456,16.8446881742378,
19.1167594559609));
#136695=CARTESIAN_POINT('Ctrl Pts',(-17.832261991049,16.8150725046001,19.1209316443614));
#136696=CARTESIAN_POINT('Ctrl Pts',(-17.9109137869838,16.7854708935318,
19.1251018522225));
#136697=CARTESIAN_POINT('Ctrl Pts',(-17.9910678502179,16.7597300059441,
19.1292720600837));
#136698=CARTESIAN_POINT('Ctrl Pts',(-18.0723097397469,16.7379925193227,
19.1334422679448));
#136699=CARTESIAN_POINT('Ctrl Pts',(-18.153537434481,16.7162588307316,19.1376117471763));
#136700=CARTESIAN_POINT('Ctrl Pts',(-18.2358521335503,16.6985272720948,
19.1417812264079));
#136701=CARTESIAN_POINT('Ctrl Pts',(-18.318825260664,16.6848903555433,19.1459507056394));
#136702=CARTESIAN_POINT('Ctrl Pts',(-18.401808780157,16.6712517309688,19.1501207070979));
#136703=CARTESIAN_POINT('Ctrl Pts',(-18.4854504373051,16.6617088401247,
19.1542907085565));
#136704=CARTESIAN_POINT('Ctrl Pts',(-18.5693138750506,16.6563026636705,
19.1584607100151));
#136705=CARTESIAN_POINT('Ctrl Pts',(-18.6532675334726,16.6508906712265,
19.1626351975806));
#136706=CARTESIAN_POINT('Ctrl Pts',(-18.737442988877,16.6496243068331,19.1668096851461));
#136707=CARTESIAN_POINT('Ctrl Pts',(-18.8214017259729,16.6524924392731,
19.1709841727116));
#136708=CARTESIAN_POINT('Ctrl Pts',(-18.9054095853483,16.6553622497897,
19.1751611026715));
#136709=CARTESIAN_POINT('Ctrl Pts',(-18.9892000156136,16.6623713344674,
19.1793380326314));
#136710=CARTESIAN_POINT('Ctrl Pts',(-19.0723398854136,16.67345667585,19.1835149625913));
#136711=CARTESIAN_POINT('Ctrl Pts',(-19.1556201623819,16.6845607382313,
19.1876989465784));
#136712=CARTESIAN_POINT('Ctrl Pts',(-19.2382472329086,16.6997547190923,
19.1918829305655));
#136713=CARTESIAN_POINT('Ctrl Pts',(-19.31979874243,16.7189245931619,19.1960669145527));
#136714=CARTESIAN_POINT('Ctrl Pts',(-19.3683964965226,16.7303482054467,
19.1985602126673));
#136715=CARTESIAN_POINT('Ctrl Pts',(-19.4166125841186,16.7431827530992,
19.2010535107819));
#136716=CARTESIAN_POINT('Ctrl Pts',(-19.4643607861717,16.7573958913422,
19.2035468088965));
#136717=CARTESIAN_POINT('Ctrl Pts',(-19.5444991251657,16.7812505547997,
19.2077314433106));
#136718=CARTESIAN_POINT('Ctrl Pts',(-19.623616676388,16.8090798944626,19.2119160777247));
#136719=CARTESIAN_POINT('Ctrl Pts',(-19.7012904347964,16.8407786570129,
19.2161007121388));
#136720=CARTESIAN_POINT('Ctrl Pts',(-19.7788536342256,16.8724323002991,
19.2202793902439));
#136721=CARTESIAN_POINT('Ctrl Pts',(-19.8549767005509,16.907944254222,19.224458068349));
#136722=CARTESIAN_POINT('Ctrl Pts',(-19.9292512406659,16.9471593537339,
19.228636746454));
#136723=CARTESIAN_POINT('Ctrl Pts',(-20.0048570980567,16.98707735547,19.2328903243342));
#136724=CARTESIAN_POINT('Ctrl Pts',(-20.0785470456703,17.0308324287623,
19.2371439022144));
#136725=CARTESIAN_POINT('Ctrl Pts',(-20.1499110578951,17.0782093688948,
19.2413974800945));
#136726=CARTESIAN_POINT('Ctrl Pts',(-20.2198915399285,17.124667814887,19.2455685940936));
#136727=CARTESIAN_POINT('Ctrl Pts',(-20.2876350664231,17.1746086809012,
19.2497397080927));
#136728=CARTESIAN_POINT('Ctrl Pts',(-20.3527809100898,17.2277833287488,
19.2539108220917));
#136729=CARTESIAN_POINT('Ctrl Pts',(-20.4179048934389,17.2809401333293,
19.2580805364332));
#136730=CARTESIAN_POINT('Ctrl Pts',(-20.4804325690375,17.337328274011,19.2622502507746));
#136731=CARTESIAN_POINT('Ctrl Pts',(-20.5400350473179,17.3966578581041,
19.2664199651161));
#136732=CARTESIAN_POINT('Ctrl Pts',(-20.5996354046852,17.455985330995,19.2705895310811));
#136733=CARTESIAN_POINT('Ctrl Pts',(-20.6563104462575,17.5182537140389,
19.2747590970462));
#136734=CARTESIAN_POINT('Ctrl Pts',(-20.7097680140135,17.58313613751,19.2789286630112));
#136735=CARTESIAN_POINT('Ctrl Pts',(-20.7651050833054,17.6502997462216,
19.2832448257251));
#136736=CARTESIAN_POINT('Ctrl Pts',(-20.8169938810693,17.7202642276976,
19.287560988439));
#136737=CARTESIAN_POINT('Ctrl Pts',(-20.865156923198,17.7926311591461,19.2918771511529));
#136738=CARTESIAN_POINT('Ctrl Pts',(-20.9117510597953,17.8626407461657,
19.2960527153652));
#136739=CARTESIAN_POINT('Ctrl Pts',(-20.9548582452776,17.9348982385166,
19.3002282795775));
#136740=CARTESIAN_POINT('Ctrl Pts',(-20.9942733140223,18.0090164119595,
19.3044038437898));
#136741=CARTESIAN_POINT('Ctrl Pts',(-21.0356791435329,18.0868781169103,
19.3087903057545));
#136742=CARTESIAN_POINT('Ctrl Pts',(-21.073009829653,18.1667928797188,19.3131767677192));
#136743=CARTESIAN_POINT('Ctrl Pts',(-21.106084856171,18.248288498498,19.3175632296839));
#136744=CARTESIAN_POINT('Ctrl Pts',(-21.1391598826889,18.3297841172771,
19.3219496916486));
#136745=CARTESIAN_POINT('Ctrl Pts',(-21.1679791313068,18.4128600189273,
19.3263361536133));
#136746=CARTESIAN_POINT('Ctrl Pts',(-21.1924232051052,18.4970284707355,
19.330722615578));
#136747=CARTESIAN_POINT('Ctrl Pts',(-21.2214742546483,18.5970601546363,
19.3359357942367));
#136748=CARTESIAN_POINT('Ctrl Pts',(-21.2444357643533,18.6989346521836,
19.3411489728953));
#136749=CARTESIAN_POINT('Ctrl Pts',(-21.2611151500594,18.8019901977457,
19.3463621515539));
#136750=CARTESIAN_POINT('Ctrl Pts',(-21.2775287210165,18.9034033756297,
19.3514922492285));
#136751=CARTESIAN_POINT('Ctrl Pts',(-21.2878587863005,19.0059603454814,
19.3566223469032));
#136752=CARTESIAN_POINT('Ctrl Pts',(-21.2919675308107,19.1090092586637,
19.3617524445778));
#136753=CARTESIAN_POINT('Ctrl Pts',(-21.2932910194166,19.1422028685647,
19.3634049264499));
#136754=CARTESIAN_POINT('Ctrl Pts',(-21.2939693565913,19.1754473495009,
19.3650574083219));
#136755=CARTESIAN_POINT('Ctrl Pts',(-21.2939989850552,19.2087204131754,
19.3667098901939));
#136756=CARTESIAN_POINT('Ctrl Pts',(-21.2939989850559,19.2087204138716,
19.3667098902285));
#136757=CARTESIAN_POINT('Ctrl Pts',(-21.294073180434,19.292042596975,19.3708480242597));
#136758=CARTESIAN_POINT('Ctrl Pts',(-21.2900751830218,19.3754486069202,
19.374986158291));
#136759=CARTESIAN_POINT('Ctrl Pts',(-21.2820071809338,19.4585063754929,
19.3791242923222));
#136760=CARTESIAN_POINT('Ctrl Pts',(-21.2739428344705,19.541526510458,19.3832605513583));
#136761=CARTESIAN_POINT('Ctrl Pts',(-21.2618121886757,19.6241982519104,
19.3873968103944));
#136762=CARTESIAN_POINT('Ctrl Pts',(-21.2456694473256,19.7060925038528,
19.3915330694305));
#136763=CARTESIAN_POINT('Ctrl Pts',(-21.2295289836483,19.7879752008609,
19.3956687448579));
#136764=CARTESIAN_POINT('Ctrl Pts',(-21.2093776397595,19.8690801670299,
19.3998044202852));
#136765=CARTESIAN_POINT('Ctrl Pts',(-21.1853208566118,19.9489878440326,
19.4039400957126));
#136766=CARTESIAN_POINT('Ctrl Pts',(-21.1612599617805,20.0289091785175,
19.4080764779921));
#136767=CARTESIAN_POINT('Ctrl Pts',(-21.1332924395122,20.1076323699233,
19.4122128602716));
#136768=CARTESIAN_POINT('Ctrl Pts',(-21.1015733410929,20.1847538059213,
19.4163492425511));
#136769=CARTESIAN_POINT('Ctrl Pts',(-21.0698191717518,20.2619605129384,
19.420490198313));
#136770=CARTESIAN_POINT('Ctrl Pts',(-21.0343053289548,20.3375614976483,
19.4246311540749));
#136771=CARTESIAN_POINT('Ctrl Pts',(-20.9952344193577,20.4111745292715,
19.4287721098369));
#136772=CARTESIAN_POINT('Ctrl Pts',(-20.956138222721,20.4848352039023,19.4329157456621));
#136773=CARTESIAN_POINT('Ctrl Pts',(-20.9134806196,20.5565049647657,19.4370593814874));
#136774=CARTESIAN_POINT('Ctrl Pts',(-20.8675081508492,20.6258296612172,
19.4412030173127));
#136775=CARTESIAN_POINT('Ctrl Pts',(-20.8214607545843,20.6952673454484,
19.4453534065784));
#136776=CARTESIAN_POINT('Ctrl Pts',(-20.7720879921639,20.7623519651645,
19.4495037958442));
#136777=CARTESIAN_POINT('Ctrl Pts',(-20.7196769297106,20.8267620897939,
19.4536541851099));
#136778=CARTESIAN_POINT('Ctrl Pts',(-20.701811538935,20.8487176082006,19.4550689308264));
#136779=CARTESIAN_POINT('Ctrl Pts',(-20.6835934338612,20.8703626873999,
19.456483676543));
#136780=CARTESIAN_POINT('Ctrl Pts',(-20.665034920053,20.8916856153177,19.4578984222595));
#136781=CARTESIAN_POINT('Ctrl Pts',(-20.6101412425939,20.9547560712659,
19.4620830566462));
#136782=CARTESIAN_POINT('Ctrl Pts',(-20.5520521994161,21.0152517076034,
19.466267691033));
#136783=CARTESIAN_POINT('Ctrl Pts',(-20.4910387353968,21.0728310563301,
19.4704523254197));
#136784=CARTESIAN_POINT('Ctrl Pts',(-20.4301121164969,21.1303284479757,
19.474631003497));
#136785=CARTESIAN_POINT('Ctrl Pts',(-20.3662696766025,21.1849174841126,
19.4788096815743));
#136786=CARTESIAN_POINT('Ctrl Pts',(-20.2998217436364,21.2362906623878,
19.4829883596516));
#136787=CARTESIAN_POINT('Ctrl Pts',(-20.2321827790938,21.2885846680655,
19.4872419375387));
#136788=CARTESIAN_POINT('Ctrl Pts',(-20.161844312329,21.3375460297091,19.4914955154257));
#136789=CARTESIAN_POINT('Ctrl Pts',(-20.0891719990913,21.3828906171534,
19.4957490933128));
#136790=CARTESIAN_POINT('Ctrl Pts',(-20.0179085806091,21.4273561111906,
19.4999202072832));
#136791=CARTESIAN_POINT('Ctrl Pts',(-19.9444014087256,21.4683435613089,
19.5040913212537));
#136792=CARTESIAN_POINT('Ctrl Pts',(-19.8690261614781,21.5056275542581,
19.5082624352241));
#136793=CARTESIAN_POINT('Ctrl Pts',(-19.793676207128,21.5428990362007,19.5124321495367));
#136794=CARTESIAN_POINT('Ctrl Pts',(-19.7164598343519,21.5764693252628,
19.5166018638493));
#136795=CARTESIAN_POINT('Ctrl Pts',(-19.6377770918877,21.6061590694939,
19.5207715781619));
#136796=CARTESIAN_POINT('Ctrl Pts',(-19.5590971492983,21.6358477572345,
19.5249411440979));
#136797=CARTESIAN_POINT('Ctrl Pts',(-19.4789513714795,21.6616560130841,
19.5291107100339));
#136798=CARTESIAN_POINT('Ctrl Pts',(-19.3977582580605,21.6834532300645,
19.5332802759699));
#136799=CARTESIAN_POINT('Ctrl Pts',(-19.313710494605,21.706016810393,19.5375964387175));
#136800=CARTESIAN_POINT('Ctrl Pts',(-19.2285408859855,21.7242819108903,
19.541912601465));
#136801=CARTESIAN_POINT('Ctrl Pts',(-19.1427269885521,21.7381609067942,
19.5462287642126));
#136802=CARTESIAN_POINT('Ctrl Pts',(-19.0597084701407,21.7515877958115,
19.5504043283956));
#136803=CARTESIAN_POINT('Ctrl Pts',(-18.9760874671013,21.7609099414407,
19.5545798925786));
#136804=CARTESIAN_POINT('Ctrl Pts',(-18.8923014001317,21.7661009112589,
19.5587554567616));
#136805=CARTESIAN_POINT('Ctrl Pts',(-18.8042834975712,21.7715540646552,
19.5631419187915));
#136806=CARTESIAN_POINT('Ctrl Pts',(-18.716084001952,21.7724477372194,19.5675283808214));
#136807=CARTESIAN_POINT('Ctrl Pts',(-18.6282074804569,21.7688131172564,
19.5719148428513));
#136808=CARTESIAN_POINT('Ctrl Pts',(-18.5403309589617,21.7651784972933,
19.5763013048811));
#136809=CARTESIAN_POINT('Ctrl Pts',(-18.4527779822413,21.7570157144011,
19.580687766911));
#136810=CARTESIAN_POINT('Ctrl Pts',(-18.3660419494175,21.7444180217665,
19.5850742289409));
#136811=CARTESIAN_POINT('Ctrl Pts',(-18.2832967675751,21.7323999672867,
19.589258863475));
#136812=CARTESIAN_POINT('Ctrl Pts',(-18.2009870108079,21.7163014146079,
19.5934434980091));
#136813=CARTESIAN_POINT('Ctrl Pts',(-18.1195464570135,21.696165355366,19.5976281325432));
#136814=CARTESIAN_POINT('Ctrl Pts',(-18.0382218237528,21.6760579573085,
19.6018068107688));
#136815=CARTESIAN_POINT('Ctrl Pts',(-17.9577643787564,21.651924577293,19.6059854889943));
#136816=CARTESIAN_POINT('Ctrl Pts',(-17.8786006574804,21.6238597068245,
19.6101641672199));
#136817=CARTESIAN_POINT('Ctrl Pts',(-17.7980179867947,21.595291794928,19.61441774507));
#136818=CARTESIAN_POINT('Ctrl Pts',(-17.7187763530359,21.5626501319716,
19.6186713229201));
#136819=CARTESIAN_POINT('Ctrl Pts',(-17.6413125871929,21.526088382307,19.6229249007702));
#136820=CARTESIAN_POINT('Ctrl Pts',(-17.565350604394,21.4902354519867,19.62709601489));
#136821=CARTESIAN_POINT('Ctrl Pts',(-17.4910986051224,21.4506132807032,
19.6312671290099));
#136822=CARTESIAN_POINT('Ctrl Pts',(-17.4189494736645,21.4074157423367,
19.6354382431297));
#136823=CARTESIAN_POINT('Ctrl Pts',(-17.346824552547,21.364232699323,19.6396079575918));
#136824=CARTESIAN_POINT('Ctrl Pts',(-17.2768014922038,21.3174769080653,
19.6437776720538));
#136825=CARTESIAN_POINT('Ctrl Pts',(-17.2092476380545,21.2673876664533,
19.6479473865159));
#136826=CARTESIAN_POINT('Ctrl Pts',(-17.1416961877673,21.2173002072362,
19.6521169526012));
#136827=CARTESIAN_POINT('Ctrl Pts',(-17.0766141380014,21.1638798081924,
19.6562865186866));
#136828=CARTESIAN_POINT('Ctrl Pts',(-17.0143378344858,21.1074076662202,
19.6604560847719));
#136829=CARTESIAN_POINT('Ctrl Pts',(-16.9498719776595,21.0489500376595,
19.6647722473428));
#136830=CARTESIAN_POINT('Ctrl Pts',(-16.8884132283835,20.987222429568,19.6690884099137));
#136831=CARTESIAN_POINT('Ctrl Pts',(-16.8302937573553,20.9225789615778,
19.6734045724845));
#136832=CARTESIAN_POINT('Ctrl Pts',(-16.7740675179232,20.8600412432427,
19.6775801368151));
#136833=CARTESIAN_POINT('Ctrl Pts',(-16.7209666048,20.794775110764,19.6817557011457));
#136834=CARTESIAN_POINT('Ctrl Pts',(-16.6712500110187,20.7271340583726,
19.6859312654763));
#136835=CARTESIAN_POINT('Ctrl Pts',(-16.6190223558411,20.6560766247986,
19.6903177271673));
#136836=CARTESIAN_POINT('Ctrl Pts',(-16.5705302090253,20.5823985401207,
19.6947041888583));
#136837=CARTESIAN_POINT('Ctrl Pts',(-16.5260204587339,20.5065409469987,
19.6990906505493));
#136838=CARTESIAN_POINT('Ctrl Pts',(-16.4815107084424,20.4306833538766,
19.7034771122403));
#136839=CARTESIAN_POINT('Ctrl Pts',(-16.4409835545861,20.3526468022858,
19.7078635739313));
#136840=CARTESIAN_POINT('Ctrl Pts',(-16.4046276535517,20.2728966388503,
19.7122500356223));
#136841=CARTESIAN_POINT('Ctrl Pts',(-16.3699445411192,20.1968158980013,
19.7164346697444));
#136842=CARTESIAN_POINT('Ctrl Pts',(-16.3389281684758,20.1188925846309,
19.7206193038666));
#136843=CARTESIAN_POINT('Ctrl Pts',(-16.3117771822155,20.0395147077777,
19.7248039379887));
#136844=CARTESIAN_POINT('Ctrl Pts',(-16.2846648420245,19.96024981551,19.728982615802));
#136845=CARTESIAN_POINT('Ctrl Pts',(-16.2614071073245,19.8795349037591,
19.7331612936152));
#136846=CARTESIAN_POINT('Ctrl Pts',(-16.2421554012761,19.7977797677242,
19.7373399714285));
#136847=CARTESIAN_POINT('Ctrl Pts',(-16.2225586206514,19.7145592229168,
19.7415935493816));
#136848=CARTESIAN_POINT('Ctrl Pts',(-16.2071130980708,19.6302612335118,
19.7458471273348));
#136849=CARTESIAN_POINT('Ctrl Pts',(-16.1959260745095,19.5453362809289,
19.7501007052879));
#136850=CARTESIAN_POINT('Ctrl Pts',(-16.1849559341096,19.462057770949,19.7542718189977));
#136851=CARTESIAN_POINT('Ctrl Pts',(-16.1780807097821,19.3781768678583,
19.7584429327075));
#136852=CARTESIAN_POINT('Ctrl Pts',(-16.175350045093,19.294128865351,19.7626140464172));
#136853=CARTESIAN_POINT('Ctrl Pts',(-16.172620296704,19.2101090659342,19.766783760471));
#136854=CARTESIAN_POINT('Ctrl Pts',(-16.1740323608365,19.125922737868,19.7709534745247));
#136855=CARTESIAN_POINT('Ctrl Pts',(-16.1795838629489,19.0420082878573,
19.7751231885784));
#136856=CARTESIAN_POINT('Ctrl Pts',(-16.1851351675175,18.9580968238458,
19.7792927542576));
#136857=CARTESIAN_POINT('Ctrl Pts',(-16.1948255859832,18.8744576776277,
19.7834623199368));
#136858=CARTESIAN_POINT('Ctrl Pts',(-16.2086007338245,18.7915258692123,
19.787631885616));
#136859=CARTESIAN_POINT('Ctrl Pts',(-16.2228602008279,18.7056782689351,
19.7919480486733));
#136860=CARTESIAN_POINT('Ctrl Pts',(-16.2414968944959,18.6205891924188,
19.7962642117307));
#136861=CARTESIAN_POINT('Ctrl Pts',(-16.2643928538834,18.5367296211091,
19.800580374788));
#136862=CARTESIAN_POINT('Ctrl Pts',(-16.2865429768018,18.4556017775032,
19.8047559387221));
#136863=CARTESIAN_POINT('Ctrl Pts',(-16.312678943375,18.3756249997159,19.8089315026562));
#136864=CARTESIAN_POINT('Ctrl Pts',(-16.3426437089087,18.2972083995474,
19.8131070665903));
#136865=CARTESIAN_POINT('Ctrl Pts',(-16.3741219298082,18.2148311468531,
19.8174935292092));
#136866=CARTESIAN_POINT('Ctrl Pts',(-16.4098256651864,18.1341763575637,
19.8218799918281));
#136867=CARTESIAN_POINT('Ctrl Pts',(-16.4495176195312,18.0556904080171,
19.826266454447));
#136868=CARTESIAN_POINT('Ctrl Pts',(-16.4892095738761,17.9772044584704,
19.830652917066));
#136869=CARTESIAN_POINT('Ctrl Pts',(-16.5328893929524,17.9008878144519,
19.8350393796849));
#136870=CARTESIAN_POINT('Ctrl Pts',(-16.5802679097329,17.8271509896836,
19.8394258423038));
#136871=CARTESIAN_POINT('Ctrl Pts',(-16.6254567089839,17.7568220980618,
19.8436095735005));
#136872=CARTESIAN_POINT('Ctrl Pts',(-16.6741780301137,17.6885781039117,
19.8477933046972));
#136873=CARTESIAN_POINT('Ctrl Pts',(-16.7262132891215,17.6227958180323,
19.8519770358939));
#136874=CARTESIAN_POINT('Ctrl Pts',(-16.7781836605484,17.5570955621741,
19.8561555500089));
#136875=CARTESIAN_POINT('Ctrl Pts',(-16.8334594864223,17.4938512802374,
19.8603340641239));
#136876=CARTESIAN_POINT('Ctrl Pts',(-16.8917781973556,17.43341207535,19.8645125782389));
#136877=CARTESIAN_POINT('Ctrl Pts',(-16.9500311212107,17.3730410495877,
19.8686863787341));
#136878=CARTESIAN_POINT('Ctrl Pts',(-17.0113197908349,17.3154691416354,
19.8728601792292));
#136879=CARTESIAN_POINT('Ctrl Pts',(-17.0753415571247,17.2610122641723,
19.8770339797244));
#136880=CARTESIAN_POINT('Ctrl Pts',(-17.1076991478945,17.2334889161351,
19.8791434830418));
#136881=CARTESIAN_POINT('Ctrl Pts',(-17.1407542697565,17.206760744079,19.8812529863593));
#136882=CARTESIAN_POINT('Ctrl Pts',(-17.174464231106,17.180864983421,19.8833624896767));
#136883=CARTESIAN_POINT('Origin',(-18.734,19.211,-1.76670989022852));
#136884=CARTESIAN_POINT('',(-17.174464231106,17.180864983421,20.7499611441365));
#136885=CARTESIAN_POINT('',(-17.1763037726969,17.1832235620119,20.6832232089404));
#136886=CARTESIAN_POINT('',(-17.174464231106,17.180864983421,-1.76670989022852));
#136887=CARTESIAN_POINT('',(-21.2939995273706,19.2094444092821,20.2332901098006));
#136888=CARTESIAN_POINT('Ctrl Pts',(-21.2939995273706,19.209444409282,20.2332901098006));
#136889=CARTESIAN_POINT('Ctrl Pts',(-21.2940497238898,19.292051655634,20.2374173417521));
#136890=CARTESIAN_POINT('Ctrl Pts',(-21.2900972916445,19.3748187808655,
20.2415445737036));
#136891=CARTESIAN_POINT('Ctrl Pts',(-21.2821221995875,19.4573194185792,
20.2456718056551));
#136892=CARTESIAN_POINT('Ctrl Pts',(-21.2739869560054,19.5414767898907,
20.249881918467));
#136893=CARTESIAN_POINT('Ctrl Pts',(-21.2616656478282,19.6253563615795,
20.254092031279));
#136894=CARTESIAN_POINT('Ctrl Pts',(-21.2451929662144,19.7085036546953,
20.2583021440909));
#136895=CARTESIAN_POINT('Ctrl Pts',(-21.2290800677258,19.7898349111956,
20.262420302989));
#136896=CARTESIAN_POINT('Ctrl Pts',(-21.2089953889688,19.8704650608503,
20.2665384618872));
#136897=CARTESIAN_POINT('Ctrl Pts',(-21.1850236968841,19.9499741790566,
20.2706566207853));
#136898=CARTESIAN_POINT('Ctrl Pts',(-21.1610629739661,20.0294469148178,
20.274772895262));
#136899=CARTESIAN_POINT('Ctrl Pts',(-21.1332189034159,20.1077991846501,
20.2788891697386));
#136900=CARTESIAN_POINT('Ctrl Pts',(-21.1016267106028,20.1846240338243,
20.2830054442153));
#136901=CARTESIAN_POINT('Ctrl Pts',(-21.0700389112288,20.2614381991786,
20.287121146253));
#136902=CARTESIAN_POINT('Ctrl Pts',(-21.0347042052762,20.3367249283834,
20.2912368482907));
#136903=CARTESIAN_POINT('Ctrl Pts',(-20.9958062168364,20.4100965922228,
20.2953525503285));
#136904=CARTESIAN_POINT('Ctrl Pts',(-20.9553538829569,20.4864001534601,
20.2996327138962));
#136905=CARTESIAN_POINT('Ctrl Pts',(-20.9110477401698,20.5606318825454,
20.3039128774639));
#136906=CARTESIAN_POINT('Ctrl Pts',(-20.8631463404351,20.6323851909359,
20.3081930410317));
#136907=CARTESIAN_POINT('Ctrl Pts',(-20.8170263796525,20.7014700149142,
20.3123140265766));
#136908=CARTESIAN_POINT('Ctrl Pts',(-20.7675741880587,20.7682571483522,
20.3164350121215));
#136909=CARTESIAN_POINT('Ctrl Pts',(-20.7150628498031,20.832416043195,20.3205559976664));
#136910=CARTESIAN_POINT('Ctrl Pts',(-20.6625158670912,20.8966184888021,
20.3246797805174));
#136911=CARTESIAN_POINT('Ctrl Pts',(-20.6069059263909,20.958188799342,20.3288035633684));
#136912=CARTESIAN_POINT('Ctrl Pts',(-20.5485433933874,21.0168328476119,
20.3329273462195));
#136913=CARTESIAN_POINT('Ctrl Pts',(-20.4900913059675,21.0755668822695,
20.3370574568111));
#136914=CARTESIAN_POINT('Ctrl Pts',(-20.4288785557237,21.1313653881747,
20.3411875674027));
#136915=CARTESIAN_POINT('Ctrl Pts',(-20.3652483070037,21.1839746478091,
20.3453176779943));
#136916=CARTESIAN_POINT('Ctrl Pts',(-20.358074893939,21.1899055998009,20.3457832897099));
#136917=CARTESIAN_POINT('Ctrl Pts',(-20.3508707850611,21.1957960645337,
20.3462489014256));
#136918=CARTESIAN_POINT('Ctrl Pts',(-20.3436364935458,21.2016457139947,
20.3467145131413));
#136919=CARTESIAN_POINT('Ctrl Pts',(-20.278618922688,21.2542189338493,20.3508991582656));
#136920=CARTESIAN_POINT('Ctrl Pts',(-20.2109019654201,21.3037012778441,
20.3550838033898));
#136921=CARTESIAN_POINT('Ctrl Pts',(-20.1408117781385,21.3498035489242,
20.3592684485141));
#136922=CARTESIAN_POINT('Ctrl Pts',(-20.0708213570877,21.3958401981249,
20.363447137223));
#136923=CARTESIAN_POINT('Ctrl Pts',(-19.9984647969504,21.4385060803063,
20.3676258259318));
#136924=CARTESIAN_POINT('Ctrl Pts',(-19.9241011364256,21.4775522903914,
20.3718045146407));
#136925=CARTESIAN_POINT('Ctrl Pts',(-19.8484048007059,21.5172982497258,
20.3760580898566));
#136926=CARTESIAN_POINT('Ctrl Pts',(-19.7706290904141,21.5532932160129,
20.3803116650725));
#136927=CARTESIAN_POINT('Ctrl Pts',(-19.6911834656511,21.5853209161957,
20.3845652402884));
#136928=CARTESIAN_POINT('Ctrl Pts',(-19.6132778082301,21.6167277941182,
20.3887363645583));
#136929=CARTESIAN_POINT('Ctrl Pts',(-19.5337668439884,21.64431965604,20.3929074888282));
#136930=CARTESIAN_POINT('Ctrl Pts',(-19.4530597043389,21.6679397920169,
20.3970786130981));
#136931=CARTESIAN_POINT('Ctrl Pts',(-19.372379649495,21.6915520012255,20.4012483375651));
#136932=CARTESIAN_POINT('Ctrl Pts',(-19.2905046576306,21.7111950025156,
20.4054180620321));
#136933=CARTESIAN_POINT('Ctrl Pts',(-19.207859856905,21.7267616810847,20.409587786499));
#136934=CARTESIAN_POINT('Ctrl Pts',(-19.1252180001543,21.7423278051371,
20.413757362432));
#136935=CARTESIAN_POINT('Ctrl Pts',(-19.0418068413031,21.7538178108621,
20.4179269383649));
#136936=CARTESIAN_POINT('Ctrl Pts',(-18.9580612092297,21.7611757928658,
20.4220965142979));
#136937=CARTESIAN_POINT('Ctrl Pts',(-18.8713716383373,21.7687924325249,
20.4264126647583));
#136938=CARTESIAN_POINT('Ctrl Pts',(-18.7843241655967,21.7719810786356,
20.4307288152187));
#136939=CARTESIAN_POINT('Ctrl Pts',(-18.6974043027306,21.7707384153349,
20.4350449656791));
#136940=CARTESIAN_POINT('Ctrl Pts',(-18.6133154147565,21.7695362255058,
20.4392205393694));
#136941=CARTESIAN_POINT('Ctrl Pts',(-18.5293464188556,21.7641870271194,
20.4433961130596));
#136942=CARTESIAN_POINT('Ctrl Pts',(-18.4459326767646,21.7547407920785,
20.4475716867499));
#136943=CARTESIAN_POINT('Ctrl Pts',(-18.3583065669897,21.7448175251454,
20.4519581255954));
#136944=CARTESIAN_POINT('Ctrl Pts',(-18.2712938435843,21.7303726259076,
20.4563445644409));
#136945=CARTESIAN_POINT('Ctrl Pts',(-18.1853859711599,21.7115244744573,
20.4607310032863));
#136946=CARTESIAN_POINT('Ctrl Pts',(-18.0994780987355,21.6926763230069,
20.4651174421318));
#136947=CARTESIAN_POINT('Ctrl Pts',(-18.0146756167237,21.6694251461088,
20.4695038809773));
#136948=CARTESIAN_POINT('Ctrl Pts',(-17.9314482086413,21.6419485025781,
20.4738903198228));
#136949=CARTESIAN_POINT('Ctrl Pts',(-17.8520491325438,21.6157357421323,
20.478074989269));
#136950=CARTESIAN_POINT('Ctrl Pts',(-17.773787899996,21.5855801451821,20.4822596587152));
#136951=CARTESIAN_POINT('Ctrl Pts',(-17.6970842255972,21.5515994268124,
20.4864443281614));
#136952=CARTESIAN_POINT('Ctrl Pts',(-17.6204897238313,21.517667073329,20.4906230415516));
#136953=CARTESIAN_POINT('Ctrl Pts',(-17.5454487937957,21.4799205972817,
20.4948017549418));
#136954=CARTESIAN_POINT('Ctrl Pts',(-17.4723650688358,21.4385271716561,
20.498980468332));
#136955=CARTESIAN_POINT('Ctrl Pts',(-17.397972153007,21.3963922417504,20.5032340374225));
#136956=CARTESIAN_POINT('Ctrl Pts',(-17.3256077133136,21.3504785638631,
20.507487606513));
#136957=CARTESIAN_POINT('Ctrl Pts',(-17.2556752275784,21.3010133653268,
20.5117411756035));
#136958=CARTESIAN_POINT('Ctrl Pts',(-17.1870977913373,21.2525066311086,
20.5159123252493));
#136959=CARTESIAN_POINT('Ctrl Pts',(-17.120859296763,21.2005850589633,20.520083474895));
#136960=CARTESIAN_POINT('Ctrl Pts',(-17.0573129692034,21.1455078445844,
20.5242546245408));
#136961=CARTESIAN_POINT('Ctrl Pts',(-16.993787964182,21.0904491109903,20.5284243745857));
#136962=CARTESIAN_POINT('Ctrl Pts',(-16.9329536794658,21.03223713911,20.5325941246305));
#136963=CARTESIAN_POINT('Ctrl Pts',(-16.8751302971831,20.9711714200467,
20.5367638746754));
#136964=CARTESIAN_POINT('Ctrl Pts',(-16.817308972357,20.910107873808,20.5409334763533));
#136965=CARTESIAN_POINT('Ctrl Pts',(-16.7624986526345,20.8461911168958,
20.5451030780312));
#136966=CARTESIAN_POINT('Ctrl Pts',(-16.7109817117549,20.77975651566,20.5492726797091));
#136967=CARTESIAN_POINT('Ctrl Pts',(-16.6576544768729,20.7109874171091,
20.5535888002753));
#136968=CARTESIAN_POINT('Ctrl Pts',(-16.6078567137602,20.6395206409879,
20.5579049208416));
#136969=CARTESIAN_POINT('Ctrl Pts',(-16.561854000255,20.5657626197204,20.5622210414078));
#136970=CARTESIAN_POINT('Ctrl Pts',(-16.517349008247,20.4944059562344,20.5663966409904));
#136971=CARTESIAN_POINT('Ctrl Pts',(-16.4763959330767,20.4209053859485,
20.5705722405729));
#136972=CARTESIAN_POINT('Ctrl Pts',(-16.4391884113254,20.3456540320665,
20.5747478401554));
#136973=CARTESIAN_POINT('Ctrl Pts',(-16.4001026787487,20.2666040401448,
20.5791342212135));
#136974=CARTESIAN_POINT('Ctrl Pts',(-16.3651508277233,20.1856223925876,
20.5835206022717));
#136975=CARTESIAN_POINT('Ctrl Pts',(-16.3344993330483,20.1031863870843,
20.5879069833298));
#136976=CARTESIAN_POINT('Ctrl Pts',(-16.3038478383734,20.0207503815809,
20.592293364388));
#136977=CARTESIAN_POINT('Ctrl Pts',(-16.2774968013516,19.9368605943871,
20.5966797454461));
#136978=CARTESIAN_POINT('Ctrl Pts',(-16.255551151987,19.8520080403421,20.6010661265042));
#136979=CARTESIAN_POINT('Ctrl Pts',(-16.2346154332719,19.7710603693828,
20.6052506479319));
#136980=CARTESIAN_POINT('Ctrl Pts',(-16.217610614143,19.6889352736661,20.6094351693596));
#136981=CARTESIAN_POINT('Ctrl Pts',(-16.2046649078707,19.6060493535286,
20.6136196907873));
#136982=CARTESIAN_POINT('Ctrl Pts',(-16.1917376291181,19.5232814170601,
20.6177982557728));
#136983=CARTESIAN_POINT('Ctrl Pts',(-16.18285805684,19.4397552579918,20.6219768207584));
#136984=CARTESIAN_POINT('Ctrl Pts',(-16.1781041141918,19.3559007277721,
20.6261553857439));
#136985=CARTESIAN_POINT('Ctrl Pts',(-16.1732647974111,19.2705402879725,
20.6304089918873));
#136986=CARTESIAN_POINT('Ctrl Pts',(-16.1727008781513,19.1848400329948,
20.6346625980307));
#136987=CARTESIAN_POINT('Ctrl Pts',(-16.1764397024494,19.0992622517103,
20.6389162041741));
#136988=CARTESIAN_POINT('Ctrl Pts',(-16.180105918999,19.0153463859165,20.6430872055358));
#136989=CARTESIAN_POINT('Ctrl Pts',(-16.1879092340601,18.9315487603075,
20.6472582068975));
#136990=CARTESIAN_POINT('Ctrl Pts',(-16.1998229072908,18.8483066546134,
20.6514292082593));
#136991=CARTESIAN_POINT('Ctrl Pts',(-16.2117325838689,18.7650924739572,
20.6555988103847));
#136992=CARTESIAN_POINT('Ctrl Pts',(-16.2277498149937,18.6824338981452,
20.6597684125102));
#136993=CARTESIAN_POINT('Ctrl Pts',(-16.2477960925062,18.6007622345655,
20.6639380146357));
#136994=CARTESIAN_POINT('Ctrl Pts',(-16.267841659387,18.5190934662099,20.6681074689506));
#136995=CARTESIAN_POINT('Ctrl Pts',(-16.2919158781826,18.4384119871214,
20.6722769232655));
#136996=CARTESIAN_POINT('Ctrl Pts',(-16.319889610317,18.3591367325534,20.6764463775805));
#136997=CARTESIAN_POINT('Ctrl Pts',(-16.3488485357305,18.2770695213162,
20.6807626738809));
#136998=CARTESIAN_POINT('Ctrl Pts',(-16.3819865976511,18.1965099318425,
20.6850789701814));
#136999=CARTESIAN_POINT('Ctrl Pts',(-16.4191057647636,18.1179013403772,
20.6893952664818));
#137000=CARTESIAN_POINT('Ctrl Pts',(-16.4550137295479,18.0418577555219,
20.6935707215798));
#137001=CARTESIAN_POINT('Ctrl Pts',(-16.4946467243009,17.9676401977748,
20.6977461766778));
#137002=CARTESIAN_POINT('Ctrl Pts',(-16.5377790112352,17.8956242481676,
20.7019216317759));
#137003=CARTESIAN_POINT('Ctrl Pts',(-16.5830936242914,17.8199645713389,
20.7063083486775));
#137004=CARTESIAN_POINT('Ctrl Pts',(-16.6322706438836,17.7467356488664,
20.7106950655792));
#137005=CARTESIAN_POINT('Ctrl Pts',(-16.68499874854,17.6763359092247,20.7150817824808));
#137006=CARTESIAN_POINT('Ctrl Pts',(-16.7377268531964,17.605936169583,20.7194684993824));
#137007=CARTESIAN_POINT('Ctrl Pts',(-16.7940056129075,17.538366010084,20.7238552162841));
#137008=CARTESIAN_POINT('Ctrl Pts',(-16.8534788424305,17.473979511942,20.7282419331857));
#137009=CARTESIAN_POINT('Ctrl Pts',(-16.9102019217452,17.4125703624776,
20.7324258003262));
#137010=CARTESIAN_POINT('Ctrl Pts',(-16.9700416925391,17.3538283670977,
20.7366096674668));
#137011=CARTESIAN_POINT('Ctrl Pts',(-17.0327174013502,17.2980866408717,
20.7407935346073));
#137012=CARTESIAN_POINT('Ctrl Pts',(-17.0784953388461,17.2573732399787,
20.7438494044504));
#137013=CARTESIAN_POINT('Ctrl Pts',(-17.1257852505876,17.2182598417392,
20.7469052742935));
#137014=CARTESIAN_POINT('Ctrl Pts',(-17.174464231106,17.180864983421,20.7499611441365));
#137015=CARTESIAN_POINT('Ctrl Pts',(-17.174464231106,17.180864983421,19.9498236312055));
#137016=CARTESIAN_POINT('Ctrl Pts',(-17.2410375710667,17.1297238011471,
19.9540083585624));
#137017=CARTESIAN_POINT('Ctrl Pts',(-17.3100351878123,17.0819328152026,
19.9581930859192));
#137018=CARTESIAN_POINT('Ctrl Pts',(-17.381077330528,17.037707509232,19.9623778132761));
#137019=CARTESIAN_POINT('Ctrl Pts',(-17.3969746033918,17.0278111050749,
19.9633142398831));
#137020=CARTESIAN_POINT('Ctrl Pts',(-17.4129741644655,17.0180930627761,
19.96425066649));
#137021=CARTESIAN_POINT('Ctrl Pts',(-17.4290716121177,17.0085554711869,
19.965187093097));
#137022=CARTESIAN_POINT('Ctrl Pts',(-17.501006718607,16.9659345736727,19.9693717283973));
#137023=CARTESIAN_POINT('Ctrl Pts',(-17.5751659817943,16.9267623274508,
19.9735563636976));
#137024=CARTESIAN_POINT('Ctrl Pts',(-17.6511848627828,16.8912777367509,
19.9777409989979));
#137025=CARTESIAN_POINT('Ctrl Pts',(-17.7270955400278,16.8558436541026,
19.9819196779726));
#137026=CARTESIAN_POINT('Ctrl Pts',(-17.8048601641239,16.8240869938583,
19.9860983569473));
#137027=CARTESIAN_POINT('Ctrl Pts',(-17.8840874845047,16.7962021376512,
19.990277035922));
#137028=CARTESIAN_POINT('Ctrl Pts',(-17.9647348762107,16.7678174729877,
19.9945306135827));
#137029=CARTESIAN_POINT('Ctrl Pts',(-18.046897502032,16.7434450254351,19.9987841912434));
#137030=CARTESIAN_POINT('Ctrl Pts',(-18.1301389337682,16.723239599019,20.0030377689041));
#137031=CARTESIAN_POINT('Ctrl Pts',(-18.2117665887586,16.7034258891629,
20.0072088837266));
#137032=CARTESIAN_POINT('Ctrl Pts',(-18.2944311263189,16.6876191861685,
20.0113799985491));
#137033=CARTESIAN_POINT('Ctrl Pts',(-18.3777050584843,16.6759154028612,
20.0155511133716));
#137034=CARTESIAN_POINT('Ctrl Pts',(-18.4609510469056,16.6642155469237,
20.0197208285176));
#137035=CARTESIAN_POINT('Ctrl Pts',(-18.5448055686335,16.6566159403141,
20.0238905436636));
#137036=CARTESIAN_POINT('Ctrl Pts',(-18.6288324772911,16.6531611090283,
20.0280602588097));
#137037=CARTESIAN_POINT('Ctrl Pts',(-18.712856395511,16.6497064006967,20.0322298255595));
#137038=CARTESIAN_POINT('Ctrl Pts',(-18.7970522287831,16.6503961924512,
20.0363993923093));
#137039=CARTESIAN_POINT('Ctrl Pts',(-18.880981635612,16.6552229364061,20.0405689590591));
#137040=CARTESIAN_POINT('Ctrl Pts',(-18.9678618596805,16.6602193805865,
20.0448851207857));
#137041=CARTESIAN_POINT('Ctrl Pts',(-19.0544560473056,16.6696490660325,
20.0492012825123));
#137042=CARTESIAN_POINT('Ctrl Pts',(-19.1402833031872,16.6834450792216,
20.0535174442389));
#137043=CARTESIAN_POINT('Ctrl Pts',(-19.2233147795964,16.6967916942552,
20.0576930091793));
#137044=CARTESIAN_POINT('Ctrl Pts',(-19.3056280709207,16.7142243988718,
20.0618685741196));
#137045=CARTESIAN_POINT('Ctrl Pts',(-19.3867996159112,16.735630802998,20.0660441390599));
#137046=CARTESIAN_POINT('Ctrl Pts',(-19.4720708905892,16.7581183799726,
20.0704305991796));
#137047=CARTESIAN_POINT('Ctrl Pts',(-19.5560814939681,16.7849914459207,
20.0748170592994));
#137048=CARTESIAN_POINT('Ctrl Pts',(-19.6383622323597,16.8160618060832,
20.0792035194192));
#137049=CARTESIAN_POINT('Ctrl Pts',(-19.7206429707512,16.8471321662457,
20.0835899795389));
#137050=CARTESIAN_POINT('Ctrl Pts',(-19.8011933431587,16.8823995182362,
20.0879764396587));
#137051=CARTESIAN_POINT('Ctrl Pts',(-19.8795742651096,16.9216202579916,
20.0923628997785));
#137052=CARTESIAN_POINT('Ctrl Pts',(-19.9543489005549,16.9590364613751,
20.0965475399714));
#137053=CARTESIAN_POINT('Ctrl Pts',(-20.0274276526341,17.0001895262269,
20.1007321801642));
#137054=CARTESIAN_POINT('Ctrl Pts',(-20.0984122381085,17.0449023003337,
20.1049168203571));
#137055=CARTESIAN_POINT('Ctrl Pts',(-20.1692957865176,17.0895514317855,
20.1090955042742));
#137056=CARTESIAN_POINT('Ctrl Pts',(-20.2380907031438,17.137749965204,20.1132741881914));
#137057=CARTESIAN_POINT('Ctrl Pts',(-20.3044217668728,17.189274134772,20.1174528721085));
#137058=CARTESIAN_POINT('Ctrl Pts',(-20.3719416499117,17.2417217469061,
20.1217064485398));
#137059=CARTESIAN_POINT('Ctrl Pts',(-20.4369080598406,17.2976151641855,
20.1259600249711));
#137060=CARTESIAN_POINT('Ctrl Pts',(-20.4989546019222,17.3566712122297,
20.1302136014024));
#137061=CARTESIAN_POINT('Ctrl Pts',(-20.5597983571728,17.4145824448741,
20.1343847212528));
#137062=CARTESIAN_POINT('Ctrl Pts',(-20.6178340905372,17.4755344539392,
20.1385558411033));
#137063=CARTESIAN_POINT('Ctrl Pts',(-20.6727497630573,17.5392197045529,
20.1427269609537));
#137064=CARTESIAN_POINT('Ctrl Pts',(-20.7276470081433,17.6028835850239,
20.1468966811484));
#137065=CARTESIAN_POINT('Ctrl Pts',(-20.7794259715033,17.6692785374397,
20.151066401343));
#137066=CARTESIAN_POINT('Ctrl Pts',(-20.8278131357729,17.7380619318977,
20.1552361215377));
#137067=CARTESIAN_POINT('Ctrl Pts',(-20.8761985781537,17.8068428786539,
20.1594056933502));
#137068=CARTESIAN_POINT('Ctrl Pts',(-20.9211921974361,17.8780117217137,
20.1635752651627));
#137069=CARTESIAN_POINT('Ctrl Pts',(-20.9625630739946,17.9511957988531,
20.1677448369751));
#137070=CARTESIAN_POINT('Ctrl Pts',(-21.0053883703184,18.0269527092786,
20.1720609927655));
#137071=CARTESIAN_POINT('Ctrl Pts',(-21.0443311966684,18.104868729537,20.1763771485559));
#137072=CARTESIAN_POINT('Ctrl Pts',(-21.0791875184544,18.1845032862763,
20.1806933043463));
#137073=CARTESIAN_POINT('Ctrl Pts',(-21.112908500301,18.2615439866305,20.1848688743318));
#137074=CARTESIAN_POINT('Ctrl Pts',(-21.1428049786358,18.3401925327768,
20.1890444443173));
#137075=CARTESIAN_POINT('Ctrl Pts',(-21.1687421896672,18.4200319413184,
20.1932200143028));
#137076=CARTESIAN_POINT('Ctrl Pts',(-21.1959893070235,18.5039034775277,
20.1976064629957));
#137077=CARTESIAN_POINT('Ctrl Pts',(-21.2188665678873,18.5890887630882,
20.2019929116885));
#137078=CARTESIAN_POINT('Ctrl Pts',(-21.2372782491424,18.6750914188312,
20.2063793603814));
#137079=CARTESIAN_POINT('Ctrl Pts',(-21.2556899303975,18.7610940745742,
20.2107658090742));
#137080=CARTESIAN_POINT('Ctrl Pts',(-21.2696360151223,18.8479135155775,
20.215152257767));
#137081=CARTESIAN_POINT('Ctrl Pts',(-21.2790836672405,18.935048687726,20.2195387064599));
#137082=CARTESIAN_POINT('Ctrl Pts',(-21.288956382332,19.0261041921328,20.2241225075637));
#137083=CARTESIAN_POINT('Ctrl Pts',(-21.2939437779116,19.1176988534549,
20.2287063086676));
#137084=CARTESIAN_POINT('Ctrl Pts',(-21.2939995273702,19.2094444086991,
20.2332901097715));
#137085=CARTESIAN_POINT('',(-21.2937660450662,19.2120076676442,20.1667099326));
#137086=CARTESIAN_POINT('Ctrl Pts',(-17.174464231106,17.180864983421,19.8833624896767));
#137087=CARTESIAN_POINT('Ctrl Pts',(-17.2411054517724,17.1296716556555,
19.8875327666645));
#137088=CARTESIAN_POINT('Ctrl Pts',(-17.3103077755869,17.08173412414,19.8917030436522));
#137089=CARTESIAN_POINT('Ctrl Pts',(-17.3817164411788,17.0373097790757,
19.89587332064));
#137090=CARTESIAN_POINT('Ctrl Pts',(-17.4531115618229,16.9928938605158,
19.9000428066007));
#137091=CARTESIAN_POINT('Ctrl Pts',(-17.5267118022329,16.951990047319,19.9042122925615));
#137092=CARTESIAN_POINT('Ctrl Pts',(-17.6021342305576,16.9148118805367,
19.9083817785222));
#137093=CARTESIAN_POINT('Ctrl Pts',(-17.6775649772729,16.8776296133492,
19.9125517243384));
#137094=CARTESIAN_POINT('Ctrl Pts',(-17.7548178977551,16.8441740106921,
19.9167216701545));
#137095=CARTESIAN_POINT('Ctrl Pts',(-17.8334875675827,16.8146116009582,
19.9208916159707));
#137096=CARTESIAN_POINT('Ctrl Pts',(-17.9122411807607,16.7850176470763,
19.9250660112681));
#137097=CARTESIAN_POINT('Ctrl Pts',(-17.9924141299049,16.7593253418245,
19.9292404065656));
#137098=CARTESIAN_POINT('Ctrl Pts',(-18.0735836975314,16.7376520043808,
19.933414801863));
#137099=CARTESIAN_POINT('Ctrl Pts',(-18.1547996667123,16.7159662771144,
19.9375915835035));
#137100=CARTESIAN_POINT('Ctrl Pts',(-18.2370129388557,16.6983041884075,
19.9417683651439));
#137101=CARTESIAN_POINT('Ctrl Pts',(-18.319790788349,16.6847318572678,19.9459451467843));
#137102=CARTESIAN_POINT('Ctrl Pts',(-18.4027096905814,16.6711363989934,
19.9501290456246));
#137103=CARTESIAN_POINT('Ctrl Pts',(-18.4861946340951,16.6616446663111,
19.9543129444648));
#137104=CARTESIAN_POINT('Ctrl Pts',(-18.5698082620909,16.6562708415172,
19.958496843305));
#137105=CARTESIAN_POINT('Ctrl Pts',(-18.6237987490351,16.6528008878227,
19.9611984451984));
#137106=CARTESIAN_POINT('Ctrl Pts',(-18.6778428604002,16.6510468155004,
19.9639000470918));
#137107=CARTESIAN_POINT('Ctrl Pts',(-18.7318236815484,16.6510009250709,
19.9666016489852));
#137108=CARTESIAN_POINT('Ctrl Pts',(-18.8154370558738,16.6509298432759,
19.970786284298));
#137109=CARTESIAN_POINT('Ctrl Pts',(-18.8992095168452,16.6549593424997,
19.9749709196109));
#137110=CARTESIAN_POINT('Ctrl Pts',(-18.9827056282392,16.6631095960615,
19.9791555549237));
#137111=CARTESIAN_POINT('Ctrl Pts',(-19.0660828933652,16.671248248757,19.9833342339317));
#137112=CARTESIAN_POINT('Ctrl Pts',(-19.1491841362882,16.6834959609934,
19.9875129129397));
#137113=CARTESIAN_POINT('Ctrl Pts',(-19.2315736415637,16.6998209002102,
19.9916915919477));
#137114=CARTESIAN_POINT('Ctrl Pts',(-19.3154398964185,16.7164384476547,
19.9959451696027));
#137115=CARTESIAN_POINT('Ctrl Pts',(-19.3985681651269,16.737280826455,20.0001987472576));
#137116=CARTESIAN_POINT('Ctrl Pts',(-19.4805039902943,16.7622591414209,
20.0044523249126));
#137117=CARTESIAN_POINT('Ctrl Pts',(-19.5608513518334,16.7867532097861,
20.0086234398184));
#137118=CARTESIAN_POINT('Ctrl Pts',(-19.6400516319826,16.8152241408901,
20.0127945547242));
#137119=CARTESIAN_POINT('Ctrl Pts',(-19.7176880447477,16.847536898824,20.0169656696301));
#137120=CARTESIAN_POINT('Ctrl Pts',(-19.7952984058592,16.8798388138977,
20.0211353848777));
#137121=CARTESIAN_POINT('Ctrl Pts',(-19.8713455174284,16.9159798188824,
20.0253051001254));
#137122=CARTESIAN_POINT('Ctrl Pts',(-19.9454312968479,16.9557762388141,
20.029474815373));
#137123=CARTESIAN_POINT('Ctrl Pts',(-20.019514439946,16.9955712426016,20.0336443822425));
#137124=CARTESIAN_POINT('Ctrl Pts',(-20.0916359848007,17.0390211842644,
20.037813949112));
#137125=CARTESIAN_POINT('Ctrl Pts',(-20.1614224652667,17.085896448252,20.0419835159816));
#137126=CARTESIAN_POINT('Ctrl Pts',(-20.233662517875,17.1344197655748,20.046299677622));
#137127=CARTESIAN_POINT('Ctrl Pts',(-20.3033998138019,17.1866134578921,
20.0506158392624));
#137128=CARTESIAN_POINT('Ctrl Pts',(-20.3702544757161,17.2421751498168,
20.0549320009028));
#137129=CARTESIAN_POINT('Ctrl Pts',(-20.43493138463,17.2959269508853,20.059107566006));
#137130=CARTESIAN_POINT('Ctrl Pts',(-20.4969102614717,17.3528303456934,
20.0632831311092));
#137131=CARTESIAN_POINT('Ctrl Pts',(-20.5558837277202,17.4125729976815,
20.0674586962125));
#137132=CARTESIAN_POINT('Ctrl Pts',(-20.6178357603199,17.4753330652,20.0718451561215));
#137133=CARTESIAN_POINT('Ctrl Pts',(-20.6764704133147,17.5412263089036,
20.0762316160305));
#137134=CARTESIAN_POINT('Ctrl Pts',(-20.7314796146231,17.6098519152917,
20.0806180759396));
#137135=CARTESIAN_POINT('Ctrl Pts',(-20.7864888159316,17.6784775216799,
20.0850045358486));
#137136=CARTESIAN_POINT('Ctrl Pts',(-20.8378722882314,17.7498349754593,
20.0893909957576));
#137137=CARTESIAN_POINT('Ctrl Pts',(-20.8853760800034,17.8234910946631,
20.0937774556667));
#137138=CARTESIAN_POINT('Ctrl Pts',(-20.9317208338504,17.8953500892083,
20.0980568909951));
#137139=CARTESIAN_POINT('Ctrl Pts',(-20.9745398785638,17.9696546343097,
20.1023363263235));
#137140=CARTESIAN_POINT('Ctrl Pts',(-21.0135728623478,18.0460332342734,
20.106615761652));
#137141=CARTESIAN_POINT('Ctrl Pts',(-21.0525424990579,18.1222878785374,
20.1108882518361));
#137142=CARTESIAN_POINT('Ctrl Pts',(-21.0877380947942,18.2006095044151,
20.1151607420202));
#137143=CARTESIAN_POINT('Ctrl Pts',(-21.118942960611,18.2805984336684,20.1194332322043));
#137144=CARTESIAN_POINT('Ctrl Pts',(-21.1500944339135,18.3604504993293,
20.1236984120223));
#137145=CARTESIAN_POINT('Ctrl Pts',(-21.1772686129624,18.4419637894576,
20.1279635918403));
#137146=CARTESIAN_POINT('Ctrl Pts',(-21.2002957124611,18.5247161966825,
20.1322287716583));
#137147=CARTESIAN_POINT('Ctrl Pts',(-21.2232995986398,18.6073851822802,
20.136489651804));
#137148=CARTESIAN_POINT('Ctrl Pts',(-21.2421646000029,18.6912903874225,
20.1407505319496));
#137149=CARTESIAN_POINT('Ctrl Pts',(-21.2567699771926,18.7759923653821,
20.1450114120952));
#137150=CARTESIAN_POINT('Ctrl Pts',(-21.271362764314,18.8606213288853,20.1492686192942));
#137151=CARTESIAN_POINT('Ctrl Pts',(-21.2817031594057,18.9460452737795,
20.1535258264931));
#137152=CARTESIAN_POINT('Ctrl Pts',(-21.2877212408942,19.0318134385456,
20.1577830336921));
#137153=CARTESIAN_POINT('Ctrl Pts',(-21.2919276409715,19.0917619812152,
20.1607586525376));
#137154=CARTESIAN_POINT('Ctrl Pts',(-21.2940234518455,19.1518784236118,
20.163734271383));
#137155=CARTESIAN_POINT('Ctrl Pts',(-21.293999801981,19.2120069046681,20.1667098902285));
#137156=CARTESIAN_POINT('Ctrl Pts',(-21.2901594272135,19.212019439545,20.166710586346));
#137157=CARTESIAN_POINT('Ctrl Pts',(-21.2914431884923,19.5768333887026,
20.1847914783466));
#137158=CARTESIAN_POINT('Ctrl Pts',(-21.0477248310816,20.7953392166858,
20.2452643059079));
#137159=CARTESIAN_POINT('Ctrl Pts',(-19.1741877278151,22.2059163556896,
20.3481290690295));
#137160=CARTESIAN_POINT('Ctrl Pts',(-16.4540142726395,21.2022206477943,
20.4753048757109));
#137161=CARTESIAN_POINT('Ctrl Pts',(-15.9020680968674,18.7161854390005,
20.5870029223479));
#137162=CARTESIAN_POINT('Ctrl Pts',(-16.7482596547722,17.5166786748788,
20.6563090334244));
#137163=CARTESIAN_POINT('Ctrl Pts',(-17.1763037726968,17.1832235620119,
20.6832232089404));
#137164=CARTESIAN_POINT('Origin',(-18.734,19.211,-1.76670989022852));
#137165=CARTESIAN_POINT('',(-17.1769962058593,17.1841776921994,21.549922496891));
#137166=CARTESIAN_POINT('',(-17.1722616694474,17.1780320626177,21.4832513372676));
#137167=CARTESIAN_POINT('',(-17.174464231106,17.180864983421,-1.76670989022852));
#137168=CARTESIAN_POINT('',(-21.2938947673487,19.209658313364,21.0332900820457));
#137169=CARTESIAN_POINT('Ctrl Pts',(-21.2904840295148,19.2096606602608,
21.0332901097715));
#137170=CARTESIAN_POINT('Ctrl Pts',(-21.288030249326,19.7238724906044,21.0587831909243));
#137171=CARTESIAN_POINT('Ctrl Pts',(-20.8878309688531,21.0966582904734,
21.1266682076376));
#137172=CARTESIAN_POINT('Ctrl Pts',(-18.6471934916355,22.2367210801752,
21.2369451599114));
#137173=CARTESIAN_POINT('Ctrl Pts',(-16.1425598602209,20.7760159325242,
21.3641209665928));
#137174=CARTESIAN_POINT('Ctrl Pts',(-16.0386997413532,18.3992339415041,
21.468446745586));
#137175=CARTESIAN_POINT('Ctrl Pts',(-16.8637709644904,17.4236621366429,
21.5303805890188));
#137176=CARTESIAN_POINT('Ctrl Pts',(-17.1769962058593,17.1841776921994,
21.549922496891));
#137177=CARTESIAN_POINT('Ctrl Pts',(-17.174464231106,17.180864983421,20.7499611441365));
#137178=CARTESIAN_POINT('Ctrl Pts',(-17.2444595711224,17.1270950442199,
20.7543551689586));
#137179=CARTESIAN_POINT('Ctrl Pts',(-17.3173285036894,17.0768805205813,
20.7587491937808));
#137180=CARTESIAN_POINT('Ctrl Pts',(-17.3926685577946,17.0305344620583,
20.7631432186029));
#137181=CARTESIAN_POINT('Ctrl Pts',(-17.4641971206759,16.9865330739424,
20.7673149474996));
#137182=CARTESIAN_POINT('Ctrl Pts',(-17.5379524259981,16.9460185574918,
20.7714866763963));
#137183=CARTESIAN_POINT('Ctrl Pts',(-17.6135585392101,16.9092157066869,
20.775658405293));
#137184=CARTESIAN_POINT('Ctrl Pts',(-17.6891339188667,16.8724278160804,
20.7798284384001));
#137185=CARTESIAN_POINT('Ctrl Pts',(-17.7665581992986,16.8393487961018,
20.7839984715072));
#137186=CARTESIAN_POINT('Ctrl Pts',(-17.8454310841992,16.8101573808614,
20.7881685046143));
#137187=CARTESIAN_POINT('Ctrl Pts',(-17.9242955646648,16.780969076162,20.7923380933764));
#137188=CARTESIAN_POINT('Ctrl Pts',(-18.0046079113321,16.7556677122338,
20.7965076821384));
#137189=CARTESIAN_POINT('Ctrl Pts',(-18.0859493836776,16.7343832757804,
20.8006772709005));
#137190=CARTESIAN_POINT('Ctrl Pts',(-18.1673065855882,16.7130947234078,
20.8048476659649));
#137191=CARTESIAN_POINT('Ctrl Pts',(-18.249692863051,16.6958247560999,20.8090180610293));
#137192=CARTESIAN_POINT('Ctrl Pts',(-18.3326772440529,16.6826527047182,
20.8131884560938));
#137193=CARTESIAN_POINT('Ctrl Pts',(-18.4157540950087,16.6694659756469,
20.8173634982524));
#137194=CARTESIAN_POINT('Ctrl Pts',(-18.4994299245131,16.6603863469597,
20.8215385404111));
#137195=CARTESIAN_POINT('Ctrl Pts',(-18.5832671191098,16.6554414311899,
20.8257135825697));
#137196=CARTESIAN_POINT('Ctrl Pts',(-18.6671584825602,16.6504933204133,
20.8298913223049));
#137197=CARTESIAN_POINT('Ctrl Pts',(-18.7512109590877,16.6496852437991,
20.8340690620401));
#137198=CARTESIAN_POINT('Ctrl Pts',(-18.8349877955741,16.6529926768781,
20.8382468017752));
#137199=CARTESIAN_POINT('Ctrl Pts',(-18.9189003990789,16.6563054699152,
20.8424313118695));
#137200=CARTESIAN_POINT('Ctrl Pts',(-19.0025360138916,16.6637470414522,
20.8466158219638));
#137201=CARTESIAN_POINT('Ctrl Pts',(-19.0854643589663,16.6752411777978,
20.8508003320581));
#137202=CARTESIAN_POINT('Ctrl Pts',(-19.1159668534451,16.679468922004,20.8523394679944));
#137203=CARTESIAN_POINT('Ctrl Pts',(-19.1463737794482,16.6842444410465,
20.8538786039308));
#137204=CARTESIAN_POINT('Ctrl Pts',(-19.1766642028218,16.6895622348469,
20.8554177398671));
#137205=CARTESIAN_POINT('Ctrl Pts',(-19.2590223527151,16.7040210508733,
20.859602573687));
#137206=CARTESIAN_POINT('Ctrl Pts',(-19.3408244952178,16.7225461130517,
20.8637874075069));
#137207=CARTESIAN_POINT('Ctrl Pts',(-19.4216382791443,16.7450815915656,
20.8679722413268));
#137208=CARTESIAN_POINT('Ctrl Pts',(-19.5023370763704,16.7675850052487,
20.8721511207141));
#137209=CARTESIAN_POINT('Ctrl Pts',(-19.5820498690828,16.7940873783028,
20.8763300001013));
#137210=CARTESIAN_POINT('Ctrl Pts',(-19.6603530717567,16.8244816182466,
20.8805088794886));
#137211=CARTESIAN_POINT('Ctrl Pts',(-19.7400550248593,16.8554187983857,
20.8847624072828));
#137212=CARTESIAN_POINT('Ctrl Pts',(-19.8182960576181,16.8903881737628,
20.8890159350769));
#137213=CARTESIAN_POINT('Ctrl Pts',(-19.8946441220391,16.9292232313445,
20.8932694628711));
#137214=CARTESIAN_POINT('Ctrl Pts',(-19.9695165810178,16.9673077103391,
20.8974407812627));
#137215=CARTESIAN_POINT('Ctrl Pts',(-20.0425681641203,17.0091095557739,
20.9016120996543));
#137216=CARTESIAN_POINT('Ctrl Pts',(-20.1134118643469,17.0544233358169,
20.9057834180459));
#137217=CARTESIAN_POINT('Ctrl Pts',(-20.1842318054824,17.0997219188245,
20.9099533374884));
#137218=CARTESIAN_POINT('Ctrl Pts',(-20.25284494715,17.1485298496368,20.9141232569309));
#137219=CARTESIAN_POINT('Ctrl Pts',(-20.3188911542426,17.2005970480514,
20.9182931763733));
#137220=CARTESIAN_POINT('Ctrl Pts',(-20.384935018117,17.2526623992016,20.9224629478735));
#137221=CARTESIAN_POINT('Ctrl Pts',(-20.4484117677876,17.3079865025997,
20.9266327193736));
#137222=CARTESIAN_POINT('Ctrl Pts',(-20.508993493609,17.3662783143125,20.9308024908737));
#137223=CARTESIAN_POINT('Ctrl Pts',(-20.5716985989686,17.4266132444502,
20.9351184121799));
#137224=CARTESIAN_POINT('Ctrl Pts',(-20.6313015884265,17.490127419461,20.9394343334862));
#137225=CARTESIAN_POINT('Ctrl Pts',(-20.6874809779157,17.5564571420112,
20.9437502547924));
#137226=CARTESIAN_POINT('Ctrl Pts',(-20.7418360321654,17.6206329135953,
20.9479260235017));
#137227=CARTESIAN_POINT('Ctrl Pts',(-20.7929861867178,17.6874437676863,
20.952101792211));
#137228=CARTESIAN_POINT('Ctrl Pts',(-20.8406829832797,17.7565286843805,
20.9562775609204));
#137229=CARTESIAN_POINT('Ctrl Pts',(-20.8907810730049,17.8290916782227,
20.9606635585251));
#137230=CARTESIAN_POINT('Ctrl Pts',(-20.9370686538008,17.9041632231126,
20.9650495561297));
#137231=CARTESIAN_POINT('Ctrl Pts',(-20.9793120563334,17.981295251012,20.9694355537344));
#137232=CARTESIAN_POINT('Ctrl Pts',(-21.021555458866,18.0584272789114,20.9738215513391));
#137233=CARTESIAN_POINT('Ctrl Pts',(-21.0597544996862,18.13761923468,20.9782075489438));
#137234=CARTESIAN_POINT('Ctrl Pts',(-21.0937343932684,18.2184005877363,
20.9825935465485));
#137235=CARTESIAN_POINT('Ctrl Pts',(-21.1297845102027,18.3041035407708,
20.9872467608424));
#137236=CARTESIAN_POINT('Ctrl Pts',(-21.1612011557346,18.3918658581185,
20.9918999751363));
#137237=CARTESIAN_POINT('Ctrl Pts',(-21.1877704304992,18.4811981951189,
20.9965531894303));
#137238=CARTESIAN_POINT('Ctrl Pts',(-21.2142564917145,18.5702507480116,
21.0011918301056));
#137239=CARTESIAN_POINT('Ctrl Pts',(-21.2359253488098,18.6608632602714,
21.0058304707809));
#137240=CARTESIAN_POINT('Ctrl Pts',(-21.2526114411354,18.7525281812567,
21.0104691114562));
#137241=CARTESIAN_POINT('Ctrl Pts',(-21.2692072331732,18.8436970382994,
21.0150826491548));
#137242=CARTESIAN_POINT('Ctrl Pts',(-21.2808739262263,18.9359066855585,
21.0196961868533));
#137243=CARTESIAN_POINT('Ctrl Pts',(-21.2874965126302,19.0286389296337,
21.0243097245519));
#137244=CARTESIAN_POINT('Ctrl Pts',(-21.2917935179279,19.0888074075896,
21.0273031767656));
#137245=CARTESIAN_POINT('Ctrl Pts',(-21.2939679583765,19.1491955214723,
21.0302966289794));
#137246=CARTESIAN_POINT('Ctrl Pts',(-21.2939996483756,19.2096582411964,
21.0332900811932));
#137247=CARTESIAN_POINT('',(-21.2964371679699,19.2128544327287,20.9667098902285));
#137248=CARTESIAN_POINT('Ctrl Pts',(-17.1763037726968,17.1832235620119,
20.6832232089404));
#137249=CARTESIAN_POINT('Ctrl Pts',(-17.4224626840759,16.9914607409853,
20.6987009689849));
#137250=CARTESIAN_POINT('Ctrl Pts',(-18.4657781420964,16.4381425114079,
20.7565706645898));
#137251=CARTESIAN_POINT('Ctrl Pts',(-20.5735369877998,16.8838680312786,
20.8510662250192));
#137252=CARTESIAN_POINT('Ctrl Pts',(-21.2904548994085,18.4784657038926,
20.9300840254041));
#137253=CARTESIAN_POINT('Ctrl Pts',(-21.2964371679699,19.2128544327287,
20.9667098902285));
#137254=CARTESIAN_POINT('Ctrl Pts',(-21.2964371679699,19.2128544327287,
20.9667098902285));
#137255=CARTESIAN_POINT('Ctrl Pts',(-21.2973789664463,19.3284704701528,
20.9724759609646));
#137256=CARTESIAN_POINT('Ctrl Pts',(-21.2376963737069,20.2931122040567,
21.0206339672611));
#137257=CARTESIAN_POINT('Ctrl Pts',(-20.0126665865687,21.9547543377114,
21.1111839091181));
#137258=CARTESIAN_POINT('Ctrl Pts',(-17.1190396137422,21.7713501236625,
21.2383597157995));
#137259=CARTESIAN_POINT('Ctrl Pts',(-15.7420433199098,19.3016368730853,
21.3623821918493));
#137260=CARTESIAN_POINT('Ctrl Pts',(-16.5519396301118,17.6604732932792,
21.4440127323387));
#137261=CARTESIAN_POINT('Ctrl Pts',(-17.1722616694474,17.1780320626177,
21.4832513372676));
#137262=CARTESIAN_POINT('Origin',(18.734,19.211,-1.76670989022852));
#137263=CARTESIAN_POINT('',(20.2955776349071,17.1782440534666,0.7498178112644));
#137264=CARTESIAN_POINT('',(20.2916906334339,17.1833020127912,0.683386617883875));
#137265=CARTESIAN_POINT('',(20.2935357313021,17.1808649545432,-1.76670989022852));
#137266=CARTESIAN_POINT('',(16.1740007446525,19.2129525932361,0.233290109771496));
#137267=CARTESIAN_POINT('Ctrl Pts',(16.1719919784605,19.2129541253863,0.233290109771496));
#137268=CARTESIAN_POINT('Ctrl Pts',(16.1708576353774,19.3442909950989,0.239839092339242));
#137269=CARTESIAN_POINT('Ctrl Pts',(16.2398215309513,20.3246257991586,0.288780010467465));
#137270=CARTESIAN_POINT('Ctrl Pts',(17.5061738855977,21.978179087,0.380112864156167));
#137271=CARTESIAN_POINT('Ctrl Pts',(20.3959079781532,21.7409373178462,0.507288670837601));
#137272=CARTESIAN_POINT('Ctrl Pts',(21.7186679484337,19.2624153691283,0.630523653207013));
#137273=CARTESIAN_POINT('Ctrl Pts',(20.9031377918545,17.6518060150516,0.711366700015944));
#137274=CARTESIAN_POINT('Ctrl Pts',(20.2955776349071,17.1782440534666,0.7498178112644));
#137275=CARTESIAN_POINT('',(19.395767528315,16.7380131948456,1.73172587381032E-11));
#137276=CARTESIAN_POINT('Ctrl Pts',(19.395767528315,16.7380131948456,1.73172587381032E-11));
#137277=CARTESIAN_POINT('Ctrl Pts',(19.3150528289901,16.7164140633987,0.0041815967549353));
#137278=CARTESIAN_POINT('Ctrl Pts',(19.2331283959629,16.6987302550736,0.00836319349255328));
#137279=CARTESIAN_POINT('Ctrl Pts',(19.1504091887632,16.685093551314,0.0125447902301714));
#137280=CARTESIAN_POINT('Ctrl Pts',(19.0678077744006,16.6714762663337,0.0167204323393492));
#137281=CARTESIAN_POINT('Ctrl Pts',(18.9844142845817,16.6618947132319,0.0208960744485263));
#137282=CARTESIAN_POINT('Ctrl Pts',(18.9006573782918,16.6564305023623,0.0250717165577041));
#137283=CARTESIAN_POINT('Ctrl Pts',(18.8165042143108,16.6509404400653,0.0292671138175207));
#137284=CARTESIAN_POINT('Ctrl Pts',(18.7319846403618,16.6496069070114,0.0334625110773381));
#137285=CARTESIAN_POINT('Ctrl Pts',(18.6475423744123,16.6524603620468,0.0376579083371547));
#137286=CARTESIAN_POINT('Ctrl Pts',(18.5636493738553,16.6552952564233,0.0418260161051873));
#137287=CARTESIAN_POINT('Ctrl Pts',(18.4798331446954,16.6622628172183,0.0459941238732202));
#137288=CARTESIAN_POINT('Ctrl Pts',(18.3965307038144,16.6733407490106,0.0501622316412529));
#137289=CARTESIAN_POINT('Ctrl Pts',(18.3132563453466,16.6844149462778,0.0543289342820943));
#137290=CARTESIAN_POINT('Ctrl Pts',(18.2304958875343,16.6995967018794,0.0584956369229356));
#137291=CARTESIAN_POINT('Ctrl Pts',(18.1486808927462,16.718811896609,0.0626623395637771));
#137292=CARTESIAN_POINT('Ctrl Pts',(18.0668688404716,16.7380264002553,0.0668288923472635));
#137293=CARTESIAN_POINT('Ctrl Pts',(17.9860026319441,16.7612739482847,0.0709954451307501));
#137294=CARTESIAN_POINT('Ctrl Pts',(17.9065019549449,16.7884296737907,0.0751619979142366));
#137295=CARTESIAN_POINT('Ctrl Pts',(17.8260462587421,16.8159116133658,0.0793786023208257));
#137296=CARTESIAN_POINT('Ctrl Pts',(17.7469895837595,16.8473961156675,0.0835952067274143));
#137297=CARTESIAN_POINT('Ctrl Pts',(17.6697476948766,16.8827029761992,0.0878118111340034));
#137298=CARTESIAN_POINT('Ctrl Pts',(17.5933154552392,16.9176397503257,0.0919842171059645));
#137299=CARTESIAN_POINT('Ctrl Pts',(17.5186605203447,16.9563188567597,0.0961566230779257));
#137300=CARTESIAN_POINT('Ctrl Pts',(17.4461607527195,16.9985194750769,0.100329029049887));
#137301=CARTESIAN_POINT('Ctrl Pts',(17.3725089964354,17.041390642215,0.10456773267379));
#137302=CARTESIAN_POINT('Ctrl Pts',(17.3010819091514,17.0878959373098,0.108806436297694));
#137303=CARTESIAN_POINT('Ctrl Pts',(17.2322432877688,17.1377593537487,0.113045139921597));
#137304=CARTESIAN_POINT('Ctrl Pts',(17.1634046663863,17.1876227701875,0.1172838435455));
#137305=CARTESIAN_POINT('Ctrl Pts',(17.0971548535428,17.2408439496524,0.121522547169403));
#137306=CARTESIAN_POINT('Ctrl Pts',(17.0338195264424,17.2971070151826,0.125761250793306));
#137307=CARTESIAN_POINT('Ctrl Pts',(16.9721381147478,17.3519008477408,0.129889266471862));
#137308=CARTESIAN_POINT('Ctrl Pts',(16.9129812130569,17.4097927309776,0.134017282150418));
#137309=CARTESIAN_POINT('Ctrl Pts',(16.8566825236081,17.4705175689386,0.138145297828974));
#137310=CARTESIAN_POINT('Ctrl Pts',(16.8004749046566,17.5311441765279,0.142266635901988));
#137311=CARTESIAN_POINT('Ctrl Pts',(16.7471166302611,17.5945942890769,0.146387973975001));
#137312=CARTESIAN_POINT('Ctrl Pts',(16.6969071786038,17.6605636623788,0.150509312048014));
#137313=CARTESIAN_POINT('Ctrl Pts',(16.6467433533799,17.7264730878598,0.154626904970446));
#137314=CARTESIAN_POINT('Ctrl Pts',(16.5997229600923,17.7948968581842,0.158744497892878));
#137315=CARTESIAN_POINT('Ctrl Pts',(16.5561068210809,17.8654958932736,0.16286209081531));
#137316=CARTESIAN_POINT('Ctrl Pts',(16.5125163943093,17.9360533093806,0.16697725636706));
#137317=CARTESIAN_POINT('Ctrl Pts',(16.4723264875143,18.0087830434683,0.171092421918811));
#137318=CARTESIAN_POINT('Ctrl Pts',(16.4357550862559,18.0833163934643,0.175207587470561));
#137319=CARTESIAN_POINT('Ctrl Pts',(16.3991935732988,18.1578295908767,0.179321640349689));
#137320=CARTESIAN_POINT('Ctrl Pts',(16.3662488306646,18.2341450104433,0.183435693228817));
#137321=CARTESIAN_POINT('Ctrl Pts',(16.3370925482536,18.3118700495687,0.187549746107944));
#137322=CARTESIAN_POINT('Ctrl Pts',(16.3079200305285,18.3896383689178,0.191666089846375));
#137323=CARTESIAN_POINT('Ctrl Pts',(16.2825403575632,18.4688174331029,0.195782433584806));
#137324=CARTESIAN_POINT('Ctrl Pts',(16.2610764229501,18.5489962371172,0.199898777323237));
#137325=CARTESIAN_POINT('Ctrl Pts',(16.239606571517,18.6291971434892,0.204016255786767));
#137326=CARTESIAN_POINT('Ctrl Pts',(16.2220547120702,18.7103978759457,0.208133734250297));
#137327=CARTESIAN_POINT('Ctrl Pts',(16.2084928021298,18.7921761784404,0.212251212713827));
#137328=CARTESIAN_POINT('Ctrl Pts',(16.1949128183452,18.874063466196,0.21637417850653));
#137329=CARTESIAN_POINT('Ctrl Pts',(16.1853334600005,18.9565293904166,0.220497144299234));
#137330=CARTESIAN_POINT('Ctrl Pts',(16.1797748247972,19.0391461249782,0.224620110091938));
#137331=CARTESIAN_POINT('Ctrl Pts',(16.1758784899859,19.0970564657531,0.227510109985124));
#137332=CARTESIAN_POINT('Ctrl Pts',(16.1739565734894,19.1550408159346,0.230400109878309));
#137333=CARTESIAN_POINT('Ctrl Pts',(16.1740007446525,19.2129525932361,0.233290109771496));
#137334=CARTESIAN_POINT('',(18.0722627314315,16.7380050975816,0.));
#137335=CARTESIAN_POINT('Origin',(18.734,19.211,0.));
#137336=CARTESIAN_POINT('',(16.1765334933267,19.2078568329122,0.166709890228504));
#137337=CARTESIAN_POINT('Ctrl Pts',(18.0722627314315,16.7380050975816,-1.38777878078145E-15));
#137338=CARTESIAN_POINT('Ctrl Pts',(17.2488902483963,16.9583275322964,0.0423919355604767));
#137339=CARTESIAN_POINT('Ctrl Pts',(16.3345567825823,17.8262089039162,0.0979618989699788));
#137340=CARTESIAN_POINT('Ctrl Pts',(16.1744956276614,18.942407731855,0.153531862379481));
#137341=CARTESIAN_POINT('Ctrl Pts',(16.1765334933267,19.2078568329122,0.166709890228504));
#137342=CARTESIAN_POINT('Ctrl Pts',(16.1765334933267,19.2078568329122,0.166709890228504));
#137343=CARTESIAN_POINT('Ctrl Pts',(16.1810511662408,19.7963216342631,0.195923797939959));
#137344=CARTESIAN_POINT('Ctrl Pts',(16.6739009423912,21.2477390833877,0.267529641211891));
#137345=CARTESIAN_POINT('Ctrl Pts',(19.0860575192109,22.2167215957953,0.381527420044302));
#137346=CARTESIAN_POINT('Ctrl Pts',(21.4520483322073,20.5433423167195,0.508703226725735));
#137347=CARTESIAN_POINT('Ctrl Pts',(21.3518777067184,18.250992735458,0.60932295933893));
#137348=CARTESIAN_POINT('Ctrl Pts',(20.5461545393492,17.3761757621948,0.667550756391643));
#137349=CARTESIAN_POINT('Ctrl Pts',(20.2916906334338,17.1833020127911,0.683386617883882));
#137350=CARTESIAN_POINT('Origin',(18.734,19.211,-1.76670989022852));
#137351=CARTESIAN_POINT('',(20.2940723354197,17.180154697314,1.55000083039626));
#137352=CARTESIAN_POINT('',(20.2935357313021,17.1808649545431,1.48324950807533));
#137353=CARTESIAN_POINT('',(20.2935357313021,17.1808649545432,-1.76670989022852));
#137354=CARTESIAN_POINT('',(16.1715629762874,19.209145560805,1.0332901097715));
#137355=CARTESIAN_POINT('Ctrl Pts',(16.1715629762874,19.209145560805,1.0332901097715));
#137356=CARTESIAN_POINT('Ctrl Pts',(16.1775452442342,19.9435342473242,1.06991597459592));
#137357=CARTESIAN_POINT('Ctrl Pts',(16.8944631203331,21.5381318465523,1.14893377498083));
#137358=CARTESIAN_POINT('Ctrl Pts',(19.6025525656016,22.1108086232828,1.27034351092621));
#137359=CARTESIAN_POINT('Ctrl Pts',(21.6424137421715,20.050299112292,1.39751931760764));
#137360=CARTESIAN_POINT('Ctrl Pts',(21.1817796660755,17.9755451208384,1.49073842409766));
#137361=CARTESIAN_POINT('Ctrl Pts',(20.4294541348775,17.2819919278148,1.5415655950272));
#137362=CARTESIAN_POINT('Ctrl Pts',(20.2940723354196,17.1801546973139,1.55000083039627));
#137363=CARTESIAN_POINT('Ctrl Pts',(20.2955776349071,17.1782440534666,0.7498178112644));
#137364=CARTESIAN_POINT('Ctrl Pts',(20.2333092697084,17.1297090584855,0.753758635576423));
#137365=CARTESIAN_POINT('Ctrl Pts',(19.4740834540712,16.5951984416462,0.800091395448925));
#137366=CARTESIAN_POINT('Ctrl Pts',(17.4553334985585,16.4672458544258,0.888816090881905));
#137367=CARTESIAN_POINT('Ctrl Pts',(16.2303037681755,18.1288878534983,0.979366032738912));
#137368=CARTESIAN_POINT('Ctrl Pts',(16.1706211779077,19.0935295300429,1.02752403903544));
#137369=CARTESIAN_POINT('Ctrl Pts',(16.1715629762874,19.209145560805,1.0332901097715));
#137370=CARTESIAN_POINT('',(16.1740711683132,19.2123417124082,0.96670991823092));
#137371=CARTESIAN_POINT('Ctrl Pts',(20.2916906334338,17.1833020127911,0.683386617883882));
#137372=CARTESIAN_POINT('Ctrl Pts',(19.8649653595043,16.8598608424138,0.709942691952123));
#137373=CARTESIAN_POINT('Ctrl Pts',(18.4990491173507,16.3489928111998,0.778890701580843));
#137374=CARTESIAN_POINT('Ctrl Pts',(16.5801690015235,17.3253417016998,0.873331792362383));
#137375=CARTESIAN_POINT('Ctrl Pts',(16.1799697185864,18.6981275092202,0.941216809075682));
#137376=CARTESIAN_POINT('Ctrl Pts',(16.1775159392447,19.2123393420905,0.966709890228504));
#137377=CARTESIAN_POINT('Ctrl Pts',(16.1740003516256,19.2123417611365,0.966709918806587));
#137378=CARTESIAN_POINT('Ctrl Pts',(16.174049215721,19.3055715198376,0.971325636241826));
#137379=CARTESIAN_POINT('Ctrl Pts',(16.17919506457,19.3986231969093,0.975941353677064));
#137380=CARTESIAN_POINT('Ctrl Pts',(16.1893550117453,19.490967647685,0.980557071112303));
#137381=CARTESIAN_POINT('Ctrl Pts',(16.1995507644016,19.5836375369126,0.985189055165875));
#137382=CARTESIAN_POINT('Ctrl Pts',(16.2147958902436,19.6755949409525,0.989821039219448));
#137383=CARTESIAN_POINT('Ctrl Pts',(16.2349566280026,19.7663217309596,0.99445302327302));
#137384=CARTESIAN_POINT('Ctrl Pts',(16.2552161964654,19.8574932761445,0.99910771394821));
#137385=CARTESIAN_POINT('Ctrl Pts',(16.2804395585911,19.9474218535553,1.0037624046234));
#137386=CARTESIAN_POINT('Ctrl Pts',(16.3104425150043,20.0356023992939,1.00841709529859));
#137387=CARTESIAN_POINT('Ctrl Pts',(16.3297568898048,20.0923685421719,1.01141354801622));
#137388=CARTESIAN_POINT('Ctrl Pts',(16.3510510137503,20.1484107097619,1.01441000073385));
#137389=CARTESIAN_POINT('Ctrl Pts',(16.3742656055452,20.2035994094432,1.01740645345148));
#137390=CARTESIAN_POINT('Ctrl Pts',(16.4066870270799,20.2806757634937,1.0215912893308));
#137391=CARTESIAN_POINT('Ctrl Pts',(16.4429490448682,20.3563053000825,1.02577612521011));
#137392=CARTESIAN_POINT('Ctrl Pts',(16.4829010312601,20.4300789281004,1.02996096108943));
#137393=CARTESIAN_POINT('Ctrl Pts',(16.5227961672129,20.5037475785304,1.03413984207691));
#137394=CARTESIAN_POINT('Ctrl Pts',(16.5663706250003,20.575565165042,1.03831872306438));
#137395=CARTESIAN_POINT('Ctrl Pts',(16.6134257496347,20.6451425482453,1.04249760405186));
#137396=CARTESIAN_POINT('Ctrl Pts',(16.6613214086794,20.7159627755642,1.04675113138857));
#137397=CARTESIAN_POINT('Ctrl Pts',(16.7128231204605,20.7844615349321,1.05100465872528));
#137398=CARTESIAN_POINT('Ctrl Pts',(16.7676724163246,20.8502546579703,1.05525818606199));
#137399=CARTESIAN_POINT('Ctrl Pts',(16.8214616326485,20.9147761886841,1.05942950491759));
#137400=CARTESIAN_POINT('Ctrl Pts',(16.878469877553,20.9766953676843,1.06360082377319));
#137401=CARTESIAN_POINT('Ctrl Pts',(16.9384107604235,21.0356805974518,1.06777214262879));
#137402=CARTESIAN_POINT('Ctrl Pts',(16.9983315346257,21.0946460391488,1.07194206211116));
#137403=CARTESIAN_POINT('Ctrl Pts',(17.0611826653049,21.150679164025,1.07611198159354));
#137404=CARTESIAN_POINT('Ctrl Pts',(17.1266402115777,21.2034845069819,1.08028190107591));
#137405=CARTESIAN_POINT('Ctrl Pts',(17.1920954288672,21.2562879711218,1.08445167219232));
#137406=CARTESIAN_POINT('Ctrl Pts',(17.2601565188202,21.3058635935363,1.08862144330872));
#137407=CARTESIAN_POINT('Ctrl Pts',(17.3304667737115,21.3519564411039,1.09279121442512));
#137408=CARTESIAN_POINT('Ctrl Pts',(17.4032413841786,21.399664830616,1.09710713490077));
#137409=CARTESIAN_POINT('Ctrl Pts',(17.4784253144497,21.4436414778788,1.10142305537642));
#137410=CARTESIAN_POINT('Ctrl Pts',(17.5555924541958,21.4836538794968,1.10573897585207));
#137411=CARTESIAN_POINT('Ctrl Pts',(17.6302537040283,21.5223669369383,1.10991474312749));
#137412=CARTESIAN_POINT('Ctrl Pts',(17.7067708828925,21.5573691217994,1.11409051040291));
#137413=CARTESIAN_POINT('Ctrl Pts',(17.78473673888,21.5884985301968,1.11826627767833));
#137414=CARTESIAN_POINT('Ctrl Pts',(17.8666278007654,21.6211951546004,1.12265227475409));
#137415=CARTESIAN_POINT('Ctrl Pts',(17.950116683959,21.6496186282125,1.12703827182985));
#137416=CARTESIAN_POINT('Ctrl Pts',(18.0347145603764,21.6736408333191,1.13142426890561));
#137417=CARTESIAN_POINT('Ctrl Pts',(18.1193124367938,21.6976630384256,1.13581026598138));
#137418=CARTESIAN_POINT('Ctrl Pts',(18.2050187243926,21.7172839196893,1.14019626305714));
#137419=CARTESIAN_POINT('Ctrl Pts',(18.2913357968955,21.7324377651034,1.1445822601329));
#137420=CARTESIAN_POINT('Ctrl Pts',(18.3736918326046,21.7468962099727,1.14876698652964));
#137421=CARTESIAN_POINT('Ctrl Pts',(18.4569101590231,21.7573423934243,1.15295171292637));
#137422=CARTESIAN_POINT('Ctrl Pts',(18.5405652833629,21.7636815332899,1.1571364393231));
#137423=CARTESIAN_POINT('Ctrl Pts',(18.6241013816905,21.7700116537136,1.16131521161602));
#137424=CARTESIAN_POINT('Ctrl Pts',(18.7080725887003,21.7722463032879,1.16549398390893));
#137425=CARTESIAN_POINT('Ctrl Pts',(18.7920441907127,21.7703418825793,1.16967275620184));
#137426=CARTESIAN_POINT('Ctrl Pts',(18.8775185285604,21.7684033808102,1.1739263108107));
#137427=CARTESIAN_POINT('Ctrl Pts',(18.9629928008506,21.7621761208413,1.17817986541955));
#137428=CARTESIAN_POINT('Ctrl Pts',(19.0480040535634,21.7516694893956,1.18243342002841));
#137429=CARTESIAN_POINT('Ctrl Pts',(19.1313696312364,21.7413662486844,1.18660463296569));
#137430=CARTESIAN_POINT('Ctrl Pts',(19.2142894786525,21.7269479022129,1.19077584590298));
#137431=CARTESIAN_POINT('Ctrl Pts',(19.2963297754537,21.7084757703806,1.19494705884027));
#137432=CARTESIAN_POINT('Ctrl Pts',(19.3783425741987,21.6900098299901,1.19911687368111));
#137433=CARTESIAN_POINT('Ctrl Pts',(19.4594759594167,21.6674929036788,1.20328668852194));
#137434=CARTESIAN_POINT('Ctrl Pts',(19.5393061675985,21.641037443421,1.20745650336278));
#137435=CARTESIAN_POINT('Ctrl Pts',(19.6191335625861,21.6145829154461,1.21162617126051));
#137436=CARTESIAN_POINT('Ctrl Pts',(19.6976574354581,21.5841902749986,1.21579583915825));
#137437=CARTESIAN_POINT('Ctrl Pts',(19.7744703683971,21.5500214647343,1.21996550705598));
#137438=CARTESIAN_POINT('Ctrl Pts',(19.853979866456,21.51465313743,1.22428155370251));
#137439=CARTESIAN_POINT('Ctrl Pts',(19.9316555794736,21.475238789784,1.22859760034904));
#137440=CARTESIAN_POINT('Ctrl Pts',(20.0070713188011,21.4320108998486,1.23291364699557));
#137441=CARTESIAN_POINT('Ctrl Pts',(20.0800341869216,21.3901889822938,1.23708931569658));
#137442=CARTESIAN_POINT('Ctrl Pts',(20.1508814665265,21.3447980820665,1.24126498439758));
#137443=CARTESIAN_POINT('Ctrl Pts',(20.2192566079351,21.2960929975867,1.24544065309859));
#137444=CARTESIAN_POINT('Ctrl Pts',(20.2910797103399,21.2449318562982,1.24982688871788));
#137445=CARTESIAN_POINT('Ctrl Pts',(20.3601743374505,21.1901138572313,1.25421312433717));
#137446=CARTESIAN_POINT('Ctrl Pts',(20.4261681137408,21.1319807585811,1.25859935995646));
#137447=CARTESIAN_POINT('Ctrl Pts',(20.492161890031,21.073847659931,1.26298559557576));
#137448=CARTESIAN_POINT('Ctrl Pts',(20.5550544538034,21.0123999213878,1.26737183119505));
#137449=CARTESIAN_POINT('Ctrl Pts',(20.6145211583455,20.948020487218,1.27175806681434));
#137450=CARTESIAN_POINT('Ctrl Pts',(20.6712532036771,20.8866016309711,1.27594259528124));
#137451=CARTESIAN_POINT('Ctrl Pts',(20.7250787538107,20.8222861461377,1.28012712374813));
#137452=CARTESIAN_POINT('Ctrl Pts',(20.7756877958407,20.7553804402786,1.28431165221502));
#137453=CARTESIAN_POINT('Ctrl Pts',(20.8262247807555,20.6885699947122,1.2884902227535));
#137454=CARTESIAN_POINT('Ctrl Pts',(20.8735540790342,20.6191770173187,1.29266879329197));
#137455=CARTESIAN_POINT('Ctrl Pts',(20.9174037187929,20.5475433778076,1.29684736383044));
#137456=CARTESIAN_POINT('Ctrl Pts',(20.9620407606535,20.4746234226361,1.30110096839983));
#137457=CARTESIAN_POINT('Ctrl Pts',(21.0030716129383,20.399381892885,1.30535457296922));
#137458=CARTESIAN_POINT('Ctrl Pts',(21.0402535236503,20.3222131589622,1.30960817753861));
#137459=CARTESIAN_POINT('Ctrl Pts',(21.0767133936984,20.2465429753506,1.31377918077288));
#137460=CARTESIAN_POINT('Ctrl Pts',(21.1094722631679,20.1690202013163,1.31795018400715));
#137461=CARTESIAN_POINT('Ctrl Pts',(21.1383468618206,20.0900427566698,1.32212118724142));
#137462=CARTESIAN_POINT('Ctrl Pts',(21.1672117644678,20.0110918324171,1.32629078986506));
#137463=CARTESIAN_POINT('Ctrl Pts',(21.1921948288651,19.9306876393951,1.3304603924887));
#137464=CARTESIAN_POINT('Ctrl Pts',(21.2131612203807,19.8492473214674,1.33462999511233));
#137465=CARTESIAN_POINT('Ctrl Pts',(21.2341268617413,19.7678099173871,1.33879944855205));
#137466=CARTESIAN_POINT('Ctrl Pts',(21.2510760020805,19.6853369078529,1.34296890199176));
#137467=CARTESIAN_POINT('Ctrl Pts',(21.2639242673564,19.6022584841778,1.34713835543148));
#137468=CARTESIAN_POINT('Ctrl Pts',(21.2772250225956,19.5162542061506,1.3514546486035));
#137469=CARTESIAN_POINT('Ctrl Pts',(21.2861305797708,19.4296015962165,1.35577094177553));
#137470=CARTESIAN_POINT('Ctrl Pts',(21.290605703432,19.342784965678,1.36008723494755));
#137471=CARTESIAN_POINT('Ctrl Pts',(21.2949348020335,19.2588011962232,1.36426268576165));
#137472=CARTESIAN_POINT('Ctrl Pts',(21.2951181996998,19.1746644168246,1.36843813657575));
#137473=CARTESIAN_POINT('Ctrl Pts',(21.2911771388899,19.0908123120325,1.37261358738984));
#137474=CARTESIAN_POINT('Ctrl Pts',(21.287036673876,19.0027175773967,1.37700030174083));
#137475=CARTESIAN_POINT('Ctrl Pts',(21.2783434334409,18.9149376655593,1.38138701609182));
#137476=CARTESIAN_POINT('Ctrl Pts',(21.2651832584911,18.8279708732557,1.38577373044281));
#137477=CARTESIAN_POINT('Ctrl Pts',(21.2520230835413,18.7410040809521,1.3901604447938));
#137478=CARTESIAN_POINT('Ctrl Pts',(21.2343961650043,18.6548509616386,1.39454715914479));
#137479=CARTESIAN_POINT('Ctrl Pts',(21.2124488481584,18.5699919602204,1.39893387349578));
#137480=CARTESIAN_POINT('Ctrl Pts',(21.1915163487695,18.489056736666,1.40311775146669));
#137481=CARTESIAN_POINT('Ctrl Pts',(21.1665762583416,18.4089973678034,1.40730162943759));
#137482=CARTESIAN_POINT('Ctrl Pts',(21.1377183903467,18.3302401576427,1.4114855074085));
#137483=CARTESIAN_POINT('Ctrl Pts',(21.108898908102,18.2515877076328,1.41566382012784));
#137484=CARTESIAN_POINT('Ctrl Pts',(21.0761721516232,18.1742344053255,1.41984213284718));
#137485=CARTESIAN_POINT('Ctrl Pts',(21.0396783460786,18.0985938851192,1.42402044556652));
#137486=CARTESIAN_POINT('Ctrl Pts',(21.0032221314464,18.0230312794007,1.42819445436126));
#137487=CARTESIAN_POINT('Ctrl Pts',(20.9630067732795,17.9491783637443,1.43236846315601));
#137488=CARTESIAN_POINT('Ctrl Pts',(20.9192209916458,17.8774298977292,1.43654247195075));
#137489=CARTESIAN_POINT('Ctrl Pts',(20.875464056581,17.8057287004162,1.44071373086123));
#137490=CARTESIAN_POINT('Ctrl Pts',(20.8281416078255,17.7361295913329,1.44488498977172));
#137491=CARTESIAN_POINT('Ctrl Pts',(20.7774882160362,17.6690026229202,1.4490562486822));
#137492=CARTESIAN_POINT('Ctrl Pts',(20.7268554210923,17.6019029498917,1.45322581146194));
#137493=CARTESIAN_POINT('Ctrl Pts',(20.6728946531877,17.5372737855256,1.45739537424168));
#137494=CARTESIAN_POINT('Ctrl Pts',(20.6158828834061,17.4754548945236,1.46156493702142));
#137495=CARTESIAN_POINT('Ctrl Pts',(20.5588584214485,17.4136222411659,1.46573542804501));
#137496=CARTESIAN_POINT('Ctrl Pts',(20.4987819085052,17.3546014533543,1.46990591906861));
#137497=CARTESIAN_POINT('Ctrl Pts',(20.4359689312939,17.2986972632686,1.47407641009221));
#137498=CARTESIAN_POINT('Ctrl Pts',(20.3899160331811,17.2577097144467,1.47713410941991));
#137499=CARTESIAN_POINT('Ctrl Pts',(20.3423929859753,17.2183967604034,1.48019180874762));
#137500=CARTESIAN_POINT('Ctrl Pts',(20.2935357313021,17.1808649545431,1.48324950807533));
#137501=CARTESIAN_POINT('Origin',(18.734,19.211,-1.76670989022852));
#137502=CARTESIAN_POINT('',(20.2935357313021,17.1808649545432,2.34989189381266));
#137503=CARTESIAN_POINT('',(20.2935357313021,17.1808649545431,2.28327545725186));
#137504=CARTESIAN_POINT('',(20.2935357313021,17.1808649545432,-1.76670989022852));
#137505=CARTESIAN_POINT('',(16.1742339456424,19.2099923322427,1.83329006740172));
#137506=CARTESIAN_POINT('Ctrl Pts',(16.174000198019,19.2099930951884,1.8332901097715));
#137507=CARTESIAN_POINT('Ctrl Pts',(16.1739663681253,19.2960037291259,1.83754657623673));
#137508=CARTESIAN_POINT('Ctrl Pts',(16.1782715498352,19.3819895204514,1.84180304270196));
#137509=CARTESIAN_POINT('Ctrl Pts',(16.1868819594924,19.4674950052547,1.84605950916719));
#137510=CARTESIAN_POINT('Ctrl Pts',(16.1954973714593,19.5530501653856,1.85031844847222));
#137511=CARTESIAN_POINT('Ctrl Pts',(16.2084229438551,19.6381240334814,1.85457738777724));
#137512=CARTESIAN_POINT('Ctrl Pts',(16.2255732751461,19.7222683894382,1.85883632708227));
#137513=CARTESIAN_POINT('Ctrl Pts',(16.2427520342423,19.8065522202146,1.86310232586009));
#137514=CARTESIAN_POINT('Ctrl Pts',(16.2641694501953,19.8899030371078,1.86736832463791));
#137515=CARTESIAN_POINT('Ctrl Pts',(16.2896893999656,19.9718848076808,1.87163432341573));
#137516=CARTESIAN_POINT('Ctrl Pts',(16.3152317962993,20.0539386868993,1.87590407443496));
#137517=CARTESIAN_POINT('Ctrl Pts',(16.3448837660451,20.1346207148683,1.88017382545418));
#137518=CARTESIAN_POINT('Ctrl Pts',(16.378460747601,20.2135142544661,1.8844435764734));
#137519=CARTESIAN_POINT('Ctrl Pts',(16.4121081360956,20.2925732244374,1.88872228065292));
#137520=CARTESIAN_POINT('Ctrl Pts',(16.4496967908718,20.3698358236637,1.89300098483243));
#137521=CARTESIAN_POINT('Ctrl Pts',(16.4909957509127,20.4449092100217,1.89727968901195));
#137522=CARTESIAN_POINT('Ctrl Pts',(16.5197685295451,20.4972124623244,1.90026064078576));
#137523=CARTESIAN_POINT('Ctrl Pts',(16.5503412786202,20.5484536572702,1.90324159255957));
#137524=CARTESIAN_POINT('Ctrl Pts',(16.5826239200438,20.5985089054101,1.90622254433338));
#137525=CARTESIAN_POINT('Ctrl Pts',(16.6279420233601,20.668776046099,1.9104071796206));
#137526=CARTESIAN_POINT('Ctrl Pts',(16.6767906254528,20.7369513808156,1.91459181490782));
#137527=CARTESIAN_POINT('Ctrl Pts',(16.728950354716,20.8026582296292,1.91877645019504));
#137528=CARTESIAN_POINT('Ctrl Pts',(16.7810358412063,20.8682715530599,1.92295512918358));
#137529=CARTESIAN_POINT('Ctrl Pts',(16.8364228098494,20.9314230124316,1.92713380817211));
#137530=CARTESIAN_POINT('Ctrl Pts',(16.8948480567165,20.9917639174008,1.93131248716064));
#137531=CARTESIAN_POINT('Ctrl Pts',(16.9543205181261,21.0531863731819,1.93556606482123));
#137532=CARTESIAN_POINT('Ctrl Pts',(17.0169409883732,21.1116961215209,1.93981964248182));
#137533=CARTESIAN_POINT('Ctrl Pts',(17.0823881640283,21.1669596987868,1.94407322014241));
#137534=CARTESIAN_POINT('Ctrl Pts',(17.146566536076,21.2211518986328,1.9482443350439));
#137535=CARTESIAN_POINT('Ctrl Pts',(17.2134626230233,21.2722223587372,1.95241544994539));
#137536=CARTESIAN_POINT('Ctrl Pts',(17.2827368115693,21.319894297471,1.95658656484688));
#137537=CARTESIAN_POINT('Ctrl Pts',(17.3519877545813,21.3675502394867,1.96075628009585));
#137538=CARTESIAN_POINT('Ctrl Pts',(17.4236148357139,21.4118096644136,1.96492599534481));
#137539=CARTESIAN_POINT('Ctrl Pts',(17.4972477392584,21.4524378968757,1.96909571059377));
#137540=CARTESIAN_POINT('Ctrl Pts',(17.5708780226965,21.4930646836486,1.97326527747024));
#137541=CARTESIAN_POINT('Ctrl Pts',(17.6465135834381,21.5300603133609,1.9774348443467));
#137542=CARTESIAN_POINT('Ctrl Pts',(17.72375887895,21.563235718915,1.98160441122317));
#137543=CARTESIAN_POINT('Ctrl Pts',(17.8037199856921,21.5975775144528,1.98592057287247));
#137544=CARTESIAN_POINT('Ctrl Pts',(17.8854056436201,21.6278252451698,1.99023673452178));
#137545=CARTESIAN_POINT('Ctrl Pts',(17.9683557183345,21.6538239465735,1.99455289617108));
#137546=CARTESIAN_POINT('Ctrl Pts',(18.0486037412687,21.6789757549798,1.99872846129521));
#137547=CARTESIAN_POINT('Ctrl Pts',(18.1300346026437,21.700151030558,2.00290402641934));
#137548=CARTESIAN_POINT('Ctrl Pts',(18.2122191472968,21.7172611080556,2.00707959154347));
#137549=CARTESIAN_POINT('Ctrl Pts',(18.2985545772998,21.7352353622707,2.01146605145537));
#137550=CARTESIAN_POINT('Ctrl Pts',(18.3857212504018,21.7487228766122,2.01585251136725));
#137551=CARTESIAN_POINT('Ctrl Pts',(18.4732153214812,21.7576824206111,2.02023897127914));
#137552=CARTESIAN_POINT('Ctrl Pts',(18.5607093925606,21.7666419646101,2.02462543119104));
#137553=CARTESIAN_POINT('Ctrl Pts',(18.6485302783064,21.7710735849926,2.02901189110292));
#137554=CARTESIAN_POINT('Ctrl Pts',(18.7361763184418,21.7709990749291,2.03339835101482));
#137555=CARTESIAN_POINT('Ctrl Pts',(18.8197896747139,21.7709279931498,2.03758298542408));
#137556=CARTESIAN_POINT('Ctrl Pts',(18.9035551457575,21.7667560675609,2.04176761983334));
#137557=CARTESIAN_POINT('Ctrl Pts',(18.9870372618431,21.7584638651253,2.0459522542426));
#137558=CARTESIAN_POINT('Ctrl Pts',(19.0704005515262,21.7501834656078,2.05013093234558));
#137559=CARTESIAN_POINT('Ctrl Pts',(19.1534808335082,21.7377944834677,2.05430961044856));
#137560=CARTESIAN_POINT('Ctrl Pts',(19.2358424472483,21.7213294919472,2.05848828855154));
#137561=CARTESIAN_POINT('Ctrl Pts',(19.3196803332538,21.7045693773805,2.06274186643257));
#137562=CARTESIAN_POINT('Ctrl Pts',(19.4027730512143,21.6835856916762,2.0669954443136));
#137563=CARTESIAN_POINT('Ctrl Pts',(19.4846662953176,21.6584681025652,2.07124902219463));
#137564=CARTESIAN_POINT('Ctrl Pts',(19.564971879664,21.6338374667537,2.07542013619847));
#137565=CARTESIAN_POINT('Ctrl Pts',(19.6441236233218,21.6052319257752,2.07959125020231));
#137566=CARTESIAN_POINT('Ctrl Pts',(19.7217049706295,21.5727872239035,2.08376236420615));
#137567=CARTESIAN_POINT('Ctrl Pts',(19.7992602848139,21.5403534091452,2.08793207855493));
#137568=CARTESIAN_POINT('Ctrl Pts',(19.8752458251399,21.5040831693519,2.09210179290371));
#137569=CARTESIAN_POINT('Ctrl Pts',(19.9492638220018,21.4641608559829,2.09627150725249));
#137570=CARTESIAN_POINT('Ctrl Pts',(20.0232791850298,21.4242399631974,2.10044107322742));
#137571=CARTESIAN_POINT('Ctrl Pts',(20.0953267393072,21.380667474352,2.10461063920235));
#137572=CARTESIAN_POINT('Ctrl Pts',(20.1650334097657,21.3336736395721,2.10878020517728));
#137573=CARTESIAN_POINT('Ctrl Pts',(20.2371908797456,21.2850275602218,2.11309636788719));
#137574=CARTESIAN_POINT('Ctrl Pts',(20.3068393549607,21.2327153644361,2.11741253059711));
#137575=CARTESIAN_POINT('Ctrl Pts',(20.3735994723772,21.1770400733913,2.12172869330702));
#137576=CARTESIAN_POINT('Ctrl Pts',(20.4381848869942,21.1231783982594,2.12590425753552));
#137577=CARTESIAN_POINT('Ctrl Pts',(20.5000669160019,21.0661697225462,2.13007982176402));
#137578=CARTESIAN_POINT('Ctrl Pts',(20.5589387125309,21.0063269049135,2.13425538599252));
#137579=CARTESIAN_POINT('Ctrl Pts',(20.6207839821297,20.9434615702666,2.13864184794314));
#137580=CARTESIAN_POINT('Ctrl Pts',(20.679306546588,20.8774687014452,2.14302830989376));
#137581=CARTESIAN_POINT('Ctrl Pts',(20.7341990153408,20.8087496359034,2.14741477184438));
#137582=CARTESIAN_POINT('Ctrl Pts',(20.7890914840937,20.7400305703616,2.151801233795));
#137583=CARTESIAN_POINT('Ctrl Pts',(20.8403535806943,20.6685858238657,2.15618769574562));
#137584=CARTESIAN_POINT('Ctrl Pts',(20.887732090256,20.5948490103337,2.16057415769625));
#137585=CARTESIAN_POINT('Ctrl Pts',(20.9329306422986,20.5245049401061,2.16475879183929));
#137586=CARTESIAN_POINT('Ctrl Pts',(20.9747633711854,20.4518132565708,2.16894342598234));
#137587=CARTESIAN_POINT('Ctrl Pts',(21.0129782252718,20.3771296020326,2.17312806012539));
#137588=CARTESIAN_POINT('Ctrl Pts',(21.0511386852003,20.3025522505172,2.17730673795496));
#137589=CARTESIAN_POINT('Ctrl Pts',(21.085691291295,20.2259889658798,2.18148541578452));
#137590=CARTESIAN_POINT('Ctrl Pts',(21.1164276176735,20.1478237008885,2.18566409361409));
#137591=CARTESIAN_POINT('Ctrl Pts',(21.147714872981,20.0682573736757,2.18991767156257));
#137592=CARTESIAN_POINT('Ctrl Pts',(21.1750474280244,19.9870314755977,2.19417124951106));
#137593=CARTESIAN_POINT('Ctrl Pts',(21.1982547719725,19.9045765414219,2.19842482745954));
#137594=CARTESIAN_POINT('Ctrl Pts',(21.2210121944986,19.8237201633461,2.20259594117414));
#137595=CARTESIAN_POINT('Ctrl Pts',(21.2398027993353,19.7416824418436,2.20676705488875));
#137596=CARTESIAN_POINT('Ctrl Pts',(21.2545152522169,19.6588871100422,2.21093816860335));
#137597=CARTESIAN_POINT('Ctrl Pts',(21.2692227681827,19.5761195610708,2.2151078826576));
#137598=CARTESIAN_POINT('Ctrl Pts',(21.2798547695702,19.492595359254,2.21927759671185));
#137599=CARTESIAN_POINT('Ctrl Pts',(21.2863509615983,19.4087487517745,2.22344731076611));
#137600=CARTESIAN_POINT('Ctrl Pts',(21.2928469224602,19.3249051279663,2.2276168764416));
#137601=CARTESIAN_POINT('Ctrl Pts',(21.295207331893,19.2407395800305,2.23178644211709));
#137602=CARTESIAN_POINT('Ctrl Pts',(21.2934238553146,19.1566904350362,2.23595600779258));
#137603=CARTESIAN_POINT('Ctrl Pts',(21.2915776736484,19.0696862139402,2.24027217084134));
#137604=CARTESIAN_POINT('Ctrl Pts',(21.2852907961475,18.9828072608782,2.2445883338901));
#137605=CARTESIAN_POINT('Ctrl Pts',(21.2746126736334,18.8965365799124,2.24890449693885));
#137606=CARTESIAN_POINT('Ctrl Pts',(21.2642823912514,18.8130761687307,2.25308006085864));
#137607=CARTESIAN_POINT('Ctrl Pts',(21.2498426885277,18.7301854650859,2.25725562477843));
#137608=CARTESIAN_POINT('Ctrl Pts',(21.231390539663,18.6482918230541,2.26143118869822));
#137609=CARTESIAN_POINT('Ctrl Pts',(21.2120064127082,18.5622619104639,2.26581765131146));
#137610=CARTESIAN_POINT('Ctrl Pts',(21.1881940056825,18.4773329923524,2.27020411392471));
#137611=CARTESIAN_POINT('Ctrl Pts',(21.1601243952751,18.3939807721656,2.27459057653795));
#137612=CARTESIAN_POINT('Ctrl Pts',(21.1320547848677,18.3106285519788,2.27897703915119));
#137613=CARTESIAN_POINT('Ctrl Pts',(21.0997282551214,18.2288535413399,2.28336350176444));
#137614=CARTESIAN_POINT('Ctrl Pts',(21.0633723464423,18.1491033611364,2.28774996437768));
#137615=CARTESIAN_POINT('Ctrl Pts',(21.0286887000586,18.073021449015,2.29193466292273));
#137616=CARTESIAN_POINT('Ctrl Pts',(20.9902091092478,17.9984989913316,2.29611936146777));
#137617=CARTESIAN_POINT('Ctrl Pts',(20.9480961900758,17.9259404445351,2.30030406001282));
#137618=CARTESIAN_POINT('Ctrl Pts',(20.906052378713,17.8535009671904,2.30448189141701));
#137619=CARTESIAN_POINT('Ctrl Pts',(20.8603873210463,17.7830193881584,2.30865972282119));
#137620=CARTESIAN_POINT('Ctrl Pts',(20.8113109120553,17.7148785561807,2.31283755422537));
#137621=CARTESIAN_POINT('Ctrl Pts',(20.7622817553091,17.6468033322485,2.31701136308764));
#137622=CARTESIAN_POINT('Ctrl Pts',(20.7098480348099,17.5810647524346,2.32118517194992));
#137623=CARTESIAN_POINT('Ctrl Pts',(20.6542641570255,17.5180187339361,2.32535898081219));
#137624=CARTESIAN_POINT('Ctrl Pts',(20.5987134202879,17.455010305673,2.32953030110402));
#137625=CARTESIAN_POINT('Ctrl Pts',(20.5400165562338,17.3946915975892,2.33370162139586));
#137626=CARTESIAN_POINT('Ctrl Pts',(20.4784688819012,17.3373862937953,2.33787294168769));
#137627=CARTESIAN_POINT('Ctrl Pts',(20.4193558194132,17.2823477884285,2.34187925906268));
#137628=CARTESIAN_POINT('Ctrl Pts',(20.3576135213163,17.2300890706105,2.34588557643767));
#137629=CARTESIAN_POINT('Ctrl Pts',(20.2935357313021,17.1808649545431,2.34989189381266));
#137630=CARTESIAN_POINT('Ctrl Pts',(20.2940723354196,17.1801546973139,1.55000083039627));
#137631=CARTESIAN_POINT('Ctrl Pts',(19.7490823055711,16.7702009552852,1.58395753058768));
#137632=CARTESIAN_POINT('Ctrl Pts',(18.1401763481965,16.3317555889403,1.66030616633957));
#137633=CARTESIAN_POINT('Ctrl Pts',(16.4202753011031,17.6266608733541,1.75473569408333));
#137634=CARTESIAN_POINT('Ctrl Pts',(16.1765569575323,18.8451666316293,1.81520852163568));
#137635=CARTESIAN_POINT('Ctrl Pts',(16.1778407186761,19.2099805598359,1.83328941362754));
#137636=CARTESIAN_POINT('',(16.1740004726294,19.2125555906437,1.76670989019937));
#137637=CARTESIAN_POINT('Ctrl Pts',(20.2935357313021,17.1808649545431,1.48324950807533));
#137638=CARTESIAN_POINT('Ctrl Pts',(20.2268277547837,17.129620347355,1.4874243831541));
#137639=CARTESIAN_POINT('Ctrl Pts',(20.157631652809,17.0816980355692,1.49159925823288));
#137640=CARTESIAN_POINT('Ctrl Pts',(20.086318576514,17.037331564471,1.49577413331165));
#137641=CARTESIAN_POINT('Ctrl Pts',(20.0149603661994,16.9929370138496,1.49995165066732));
#137642=CARTESIAN_POINT('Ctrl Pts',(19.9414829166633,16.9521030063531,1.50412916802298));
#137643=CARTESIAN_POINT('Ctrl Pts',(19.866281573762,16.9150168908027,1.50830668537865));
#137644=CARTESIAN_POINT('Ctrl Pts',(19.7909572166317,16.8778701098476,1.51249103631011));
#137645=CARTESIAN_POINT('Ctrl Pts',(19.7139037594437,16.8444836393503,1.51667538724156));
#137646=CARTESIAN_POINT('Ctrl Pts',(19.6355356364855,16.814996348887,1.52085973817302));
#137647=CARTESIAN_POINT('Ctrl Pts',(19.6027604934786,16.8026641642521,1.52260971884108));
#137648=CARTESIAN_POINT('Ctrl Pts',(19.5697555724601,16.7910133725809,1.52435969950915));
#137649=CARTESIAN_POINT('Ctrl Pts',(19.5365517913736,16.7800514974268,1.52610968017721));
#137650=CARTESIAN_POINT('Ctrl Pts',(19.457153209384,16.7538389001049,1.53029432358246));
#137651=CARTESIAN_POINT('Ctrl Pts',(19.3763213117682,16.7314715386277,1.53447896698771));
#137652=CARTESIAN_POINT('Ctrl Pts',(19.2944633944868,16.713104729289,1.53866361039297));
#137653=CARTESIAN_POINT('Ctrl Pts',(19.2127219865111,16.6947640616392,1.54284229774762));
#137654=CARTESIAN_POINT('Ctrl Pts',(19.1299579046074,16.6804127358414,1.54702098510228));
#137655=CARTESIAN_POINT('Ctrl Pts',(19.0465949713152,16.670156757313,1.55119967245693));
#137656=CARTESIAN_POINT('Ctrl Pts',(18.9617380512092,16.6597169765107,1.555453248057));
#137657=CARTESIAN_POINT('Ctrl Pts',(18.8762610609814,16.6535209330019,1.55970682365707));
#137658=CARTESIAN_POINT('Ctrl Pts',(18.7906234644726,16.6516262908143,1.56396039925714));
#137659=CARTESIAN_POINT('Ctrl Pts',(18.7066458766309,16.6497683745809,1.5681315230761));
#137660=CARTESIAN_POINT('Ctrl Pts',(18.622514334468,16.6520466005142,1.57230264689506));
#137661=CARTESIAN_POINT('Ctrl Pts',(18.5386669502935,16.6584630267727,1.57647377071402));
#137662=CARTESIAN_POINT('Ctrl Pts',(18.4548476979935,16.6648773002377,1.58064349506736));
#137663=CARTESIAN_POINT('Ctrl Pts',(18.3713128726456,16.6754269815325,1.58481321942069));
#137664=CARTESIAN_POINT('Ctrl Pts',(18.288498029712,16.6900620804015,1.58898294377403));
#137665=CARTESIAN_POINT('Ctrl Pts',(18.2056861301166,16.7046966591217,1.5931525199304));
#137666=CARTESIAN_POINT('Ctrl Pts',(18.1235946149205,16.7234162858241,1.59732209608676));
#137667=CARTESIAN_POINT('Ctrl Pts',(18.0426500224208,16.7461196360673,1.60149167224312));
#137668=CARTESIAN_POINT('Ctrl Pts',(17.9588599467864,16.7696210878046,1.60580782346108));
#137669=CARTESIAN_POINT('Ctrl Pts',(17.8762994412696,16.7973914245207,1.61012397467904));
#137670=CARTESIAN_POINT('Ctrl Pts',(17.7954238786637,16.8292622175274,1.614440125897));
#137671=CARTESIAN_POINT('Ctrl Pts',(17.7171824223146,16.8600949830687,1.61861570064709));
#137672=CARTESIAN_POINT('Ctrl Pts',(17.640518246769,16.894764965485,1.62279127539718));
#137673=CARTESIAN_POINT('Ctrl Pts',(17.5658209824088,16.9330716027803,1.62696685014727));
#137674=CARTESIAN_POINT('Ctrl Pts',(17.4873515388116,16.9733127085343,1.63135328959917));
#137675=CARTESIAN_POINT('Ctrl Pts',(17.4110533973333,17.0175671442341,1.63573972905106));
#137676=CARTESIAN_POINT('Ctrl Pts',(17.3373445043262,17.0655505304473,1.64012616850296));
#137677=CARTESIAN_POINT('Ctrl Pts',(17.263635611319,17.1135339166605,1.64451260795485));
#137678=CARTESIAN_POINT('Ctrl Pts',(17.1925163913081,17.1652458506637,1.64889904740675));
#137679=CARTESIAN_POINT('Ctrl Pts',(17.1243635063082,17.2203542861233,1.65328548685865));
#137680=CARTESIAN_POINT('Ctrl Pts',(17.0601943716838,17.27224146029,1.65741552513525));
#137681=CARTESIAN_POINT('Ctrl Pts',(16.9984022161797,17.3273436089106,1.66154556341186));
#137682=CARTESIAN_POINT('Ctrl Pts',(16.9393333495131,17.3854119814071,1.66567560168847));
#137683=CARTESIAN_POINT('Ctrl Pts',(16.8791242534032,17.4446012704164,1.66988536370976));
#137684=CARTESIAN_POINT('Ctrl Pts',(16.8217451257373,17.5068722664466,1.67409512573104));
#137685=CARTESIAN_POINT('Ctrl Pts',(16.7675298311078,17.5719163917429,1.67830488775233));
#137686=CARTESIAN_POINT('Ctrl Pts',(16.7144792339723,17.6355631857096,1.6824242122078));
#137687=CARTESIAN_POINT('Ctrl Pts',(16.6644582224381,17.701864774228,1.68654353666328));
#137688=CARTESIAN_POINT('Ctrl Pts',(16.6177431433907,17.7704942149182,1.69066286111875));
#137689=CARTESIAN_POINT('Ctrl Pts',(16.5710563616802,17.8390820837981,1.69477969032184));
#137690=CARTESIAN_POINT('Ctrl Pts',(16.5276718045391,17.9099946168291,1.69889651952493));
#137691=CARTESIAN_POINT('Ctrl Pts',(16.4878244173549,17.9828732752973,1.70301334872802));
#137692=CARTESIAN_POINT('Ctrl Pts',(16.4479884744815,18.0557310027567,1.70712899556318));
#137693=CARTESIAN_POINT('Ctrl Pts',(16.4116879110196,18.1305533194009,1.71124464239834));
#137694=CARTESIAN_POINT('Ctrl Pts',(16.3791125474012,18.206955635645,1.7153602892335));
#137695=CARTESIAN_POINT('Ctrl Pts',(16.3452431867613,18.2863928948241,1.71963942264732));
#137696=CARTESIAN_POINT('Ctrl Pts',(16.3154014151592,18.367537815818,1.72391855606114));
#137697=CARTESIAN_POINT('Ctrl Pts',(16.2897454150196,18.4499352696373,1.72819768947497));
#137698=CARTESIAN_POINT('Ctrl Pts',(16.265047031356,18.529257218353,1.73231710318821));
#137699=CARTESIAN_POINT('Ctrl Pts',(16.2442275674438,18.6097393677812,1.73643651690145));
#137700=CARTESIAN_POINT('Ctrl Pts',(16.2273766224859,18.690962267427,1.74055593061469));
#137701=CARTESIAN_POINT('Ctrl Pts',(16.2105163819041,18.7722299727216,1.74467761675363));
#137702=CARTESIAN_POINT('Ctrl Pts',(16.1976290874525,18.8542387741595,1.74879930289257));
#137703=CARTESIAN_POINT('Ctrl Pts',(16.1887526583662,18.9365624480759,1.75292098903151));
#137704=CARTESIAN_POINT('Ctrl Pts',(16.1798641545679,19.018998107865,1.75704828194913));
#137705=CARTESIAN_POINT('Ctrl Pts',(16.1749974202386,19.1017490235124,1.76117557486675));
#137706=CARTESIAN_POINT('Ctrl Pts',(16.1741383212113,19.1843882456639,1.76530286778437));
#137707=CARTESIAN_POINT('Ctrl Pts',(16.1740406969644,19.1937790045501,1.76577187525603));
#137708=CARTESIAN_POINT('Ctrl Pts',(16.173994768433,19.2031683266851,1.7662408827277));
#137709=CARTESIAN_POINT('Ctrl Pts',(16.1740004726294,19.2125555906437,1.76670989019937));
#137710=CARTESIAN_POINT('Ctrl Pts',(16.1740004726297,19.2125555912267,1.7667098902285));
#137711=CARTESIAN_POINT('Ctrl Pts',(16.1740562220857,19.3043011464569,1.77129369133236));
#137712=CARTESIAN_POINT('Ctrl Pts',(16.1790436176611,19.3958958077681,1.77587749243622));
#137713=CARTESIAN_POINT('Ctrl Pts',(16.188916332748,19.4869513121681,1.78046129354008));
#137714=CARTESIAN_POINT('Ctrl Pts',(16.1979293239672,19.5700776309547,1.78464593360467));
#137715=CARTESIAN_POINT('Ctrl Pts',(16.2110359189468,19.6529166093026,1.78883057366926));
#137716=CARTESIAN_POINT('Ctrl Pts',(16.2282088654964,19.7350331957452,1.79301521373385));
#137717=CARTESIAN_POINT('Ctrl Pts',(16.2453573687607,19.8170329007231,1.79719389754915));
#137718=CARTESIAN_POINT('Ctrl Pts',(16.2665606336754,19.898311809733,1.80137258136445));
#137719=CARTESIAN_POINT('Ctrl Pts',(16.2917396796525,19.9784402437038,1.80555126517975));
#137720=CARTESIAN_POINT('Ctrl Pts',(16.3173699981905,20.0600047830626,1.80980484163982));
#137721=CARTESIAN_POINT('Ctrl Pts',(16.3471199654275,20.1403767219199,1.8140584180999));
#137722=CARTESIAN_POINT('Ctrl Pts',(16.3808518403883,20.2191139513548,1.81831199455997));
#137723=CARTESIAN_POINT('Ctrl Pts',(16.4139298144973,20.2963248398595,1.82248311437409));
#137724=CARTESIAN_POINT('Ctrl Pts',(16.450836503808,20.3719633895875,1.82665423418821));
#137725=CARTESIAN_POINT('Ctrl Pts',(16.4913923918018,20.4456299508969,1.83082535400233));
#137726=CARTESIAN_POINT('Ctrl Pts',(16.5319346711508,20.5192717931798,1.8349950741852));
#137727=CARTESIAN_POINT('Ctrl Pts',(16.5761234956298,20.5909425585429,1.83916479436806));
#137728=CARTESIAN_POINT('Ctrl Pts',(16.6237330294819,20.6602664741656,1.84333451455093));
#137729=CARTESIAN_POINT('Ctrl Pts',(16.671340869397,20.7295879232582,1.84750408637604));
#137730=CARTESIAN_POINT('Ctrl Pts',(16.7223689155627,20.7965623098985,1.85167365820116));
#137731=CARTESIAN_POINT('Ctrl Pts',(16.7765483378666,20.8608433229889,1.85584323002627));
#137732=CARTESIAN_POINT('Ctrl Pts',(16.8326324731959,20.9273841771355,1.86015938587588));
#137733=CARTESIAN_POINT('Ctrl Pts',(16.8920933523659,20.9910383498724,1.86447554172548));
#137734=CARTESIAN_POINT('Ctrl Pts',(16.9545891221584,21.0514610639237,1.86879169757509));
#137735=CARTESIAN_POINT('Ctrl Pts',(17.0150492802823,21.1099156898598,1.872967267634));
#137736=CARTESIAN_POINT('Ctrl Pts',(17.0783492738879,21.1653458606137,1.87714283769291));
#137737=CARTESIAN_POINT('Ctrl Pts',(17.1441452212348,21.2174799481773,1.88131840775181));
#137738=CARTESIAN_POINT('Ctrl Pts',(17.2132640592835,21.2722469619589,1.88570485649677));
#137739=CARTESIAN_POINT('Ctrl Pts',(17.2851371185139,21.323375865423,1.89009130524172));
#137740=CARTESIAN_POINT('Ctrl Pts',(17.3593324933327,21.3706039558477,1.89447775398667));
#137741=CARTESIAN_POINT('Ctrl Pts',(17.4335278681516,21.4178320462725,1.89886420273162));
#137742=CARTESIAN_POINT('Ctrl Pts',(17.5100450161993,21.4611591039616,1.90325065147657));
#137743=CARTESIAN_POINT('Ctrl Pts',(17.5884257348941,21.5003797420103,1.90763710022152));
#137744=CARTESIAN_POINT('Ctrl Pts',(17.6632002791351,21.5377958997562,1.91182173531038));
#137745=CARTESIAN_POINT('Ctrl Pts',(17.7399490034729,21.5716144630813,1.91600637039924));
#137746=CARTESIAN_POINT('Ctrl Pts',(17.818291348554,21.6016228614457,1.9201910054881));
#137747=CARTESIAN_POINT('Ctrl Pts',(17.8965221835546,21.6315885467804,1.92436968429629));
#137748=CARTESIAN_POINT('Ctrl Pts',(17.9763417077984,21.6577546763325,1.92854836310447));
#137749=CARTESIAN_POINT('Ctrl Pts',(18.0573458795764,21.679955082887,1.93272704191266));
#137750=CARTESIAN_POINT('Ctrl Pts',(18.1398019751846,21.7025534109142,1.93698061962059));
#137751=CARTESIAN_POINT('Ctrl Pts',(18.22348517397,21.7210422324029,1.94123419732852));
#137752=CARTESIAN_POINT('Ctrl Pts',(18.3079491747639,21.7352980597219,1.94548777503645));
#137753=CARTESIAN_POINT('Ctrl Pts',(18.3907756952125,21.7492775132387,1.94965888980362));
#137754=CARTESIAN_POINT('Ctrl Pts',(18.4743525389348,21.759186555656,1.95383000457078));
#137755=CARTESIAN_POINT('Ctrl Pts',(18.5582464958671,21.7649598089604,1.95800111933795));
#137756=CARTESIAN_POINT('Ctrl Pts',(18.6421123018319,21.7707311250256,1.96217083447015));
#137757=CARTESIAN_POINT('Ctrl Pts',(18.7262945511122,21.772369376577,1.96634054960234));
#137758=CARTESIAN_POINT('Ctrl Pts',(18.8103550385056,21.769861056817,1.97051026473454));
#137759=CARTESIAN_POINT('Ctrl Pts',(18.8944125351025,21.7673528263009,1.97467983151203));
#137760=CARTESIAN_POINT('Ctrl Pts',(18.9783478186234,21.7606983323763,1.97884939828952));
#137761=CARTESIAN_POINT('Ctrl Pts',(19.0617241844592,21.7499361667676,1.983018965067));
#137762=CARTESIAN_POINT('Ctrl Pts',(19.1480319248283,21.7387956212922,1.98733512688666));
#137763=CARTESIAN_POINT('Ctrl Pts',(19.2337401905613,21.7232532494629,1.99165128870633));
#137764=CARTESIAN_POINT('Ctrl Pts',(19.3183740371403,21.7034098749436,1.99596745052599));
#137765=CARTESIAN_POINT('Ctrl Pts',(19.4002509797481,21.6842128881312,2.00014301559692));
#137766=CARTESIAN_POINT('Ctrl Pts',(19.4811219860911,21.6609909777928,2.00431858066786));
#137767=CARTESIAN_POINT('Ctrl Pts',(19.5605725242402,21.6338862668667,2.00849414573879));
#137768=CARTESIAN_POINT('Ctrl Pts',(19.6440358680187,21.6054125792273,2.01288060593282));
#137769=CARTESIAN_POINT('Ctrl Pts',(19.7259309366151,21.572653764432,2.01726706612684));
#137770=CARTESIAN_POINT('Ctrl Pts',(19.8058030522818,21.5358307932233,2.02165352632086));
#137771=CARTESIAN_POINT('Ctrl Pts',(19.8856751679486,21.4990078220147,2.02603998651489));
#137772=CARTESIAN_POINT('Ctrl Pts',(19.9635238523773,21.4581210315221,2.03042644670891));
#137773=CARTESIAN_POINT('Ctrl Pts',(20.0389283879064,21.4134445287989,2.03481290690294));
#137774=CARTESIAN_POINT('Ctrl Pts',(20.1108634458295,21.3708236600586,2.03899753937791));
#137775=CARTESIAN_POINT('Ctrl Pts',(20.1808420875566,21.3245955126394,2.04318217185287));
#137776=CARTESIAN_POINT('Ctrl Pts',(20.2484795854888,21.274965015483,2.04736680432784));
#137777=CARTESIAN_POINT('Ctrl Pts',(20.316020809252,21.225405161609,2.05154548046162));
#137778=CARTESIAN_POINT('Ctrl Pts',(20.3812271405885,21.1724528472506,2.0557241565954));
#137779=CARTESIAN_POINT('Ctrl Pts',(20.4437401591169,21.1163578635792,2.05990283272918));
#137780=CARTESIAN_POINT('Ctrl Pts',(20.5073737155061,21.0592573845008,2.06415641109815));
#137781=CARTESIAN_POINT('Ctrl Pts',(20.5682160360671,20.9989007052303,2.06840998946712));
#137782=CARTESIAN_POINT('Ctrl Pts',(20.6259217120567,20.9355962528802,2.07266356783608));
#137783=CARTESIAN_POINT('Ctrl Pts',(20.6825086171466,20.8735191179108,2.07683467979915));
#137784=CARTESIAN_POINT('Ctrl Pts',(20.7360790917207,20.8086078455881,2.08100579176223));
#137785=CARTESIAN_POINT('Ctrl Pts',(20.7863436748012,20.7411913084655,2.0851769037253));
#137786=CARTESIAN_POINT('Ctrl Pts',(20.8365913908688,20.6737973939438,2.089346616011));
#137787=CARTESIAN_POINT('Ctrl Pts',(20.8835351438624,20.6039002527225,2.0935163282967));
#137788=CARTESIAN_POINT('Ctrl Pts',(20.9269263844747,20.5318610344297,2.0976860405824));
#137789=CARTESIAN_POINT('Ctrl Pts',(20.9703160808612,20.459824379899,2.10185560447463));
#137790=CARTESIAN_POINT('Ctrl Pts',(21.0101532796088,20.3856461943776,2.10602516836686));
#137791=CARTESIAN_POINT('Ctrl Pts',(21.0462340502372,20.3097145657193,2.11019473225908));
#137792=CARTESIAN_POINT('Ctrl Pts',(21.0835834151515,20.2311131928022,2.11451089736952));
#137793=CARTESIAN_POINT('Ctrl Pts',(21.1169070503632,20.1506332529357,2.11882706247996));
#137794=CARTESIAN_POINT('Ctrl Pts',(21.146032653323,20.0687286746423,2.12314322759041));
#137795=CARTESIAN_POINT('Ctrl Pts',(21.1742094633538,19.989492212262,2.12731878970826));
#137796=CARTESIAN_POINT('Ctrl Pts',(21.1984574605128,19.9089229687612,2.13149435182612));
#137797=CARTESIAN_POINT('Ctrl Pts',(21.2186717693869,19.8274464278522,2.13566991394397));
#137798=CARTESIAN_POINT('Ctrl Pts',(21.2399070877349,19.741854568399,2.14005638055071));
#137799=CARTESIAN_POINT('Ctrl Pts',(21.2566904008882,19.6552619177352,2.14444284715744));
#137800=CARTESIAN_POINT('Ctrl Pts',(21.2689614014552,19.568170397895,2.14882931376417));
#137801=CARTESIAN_POINT('Ctrl Pts',(21.2812324020222,19.4810788780547,2.15321578037091));
#137802=CARTESIAN_POINT('Ctrl Pts',(21.2889911145764,19.3934890737086,2.15760224697764));
#137803=CARTESIAN_POINT('Ctrl Pts',(21.292240293453,19.3059031135093,2.16198871358438));
#137804=CARTESIAN_POINT('Ctrl Pts',(21.2953400676656,19.2223445557526,2.16617348044054));
#137805=CARTESIAN_POINT('Ctrl Pts',(21.2943474565447,19.1384784653558,2.17035824729669));
#137806=CARTESIAN_POINT('Ctrl Pts',(21.2892265251101,19.0547393031703,2.17454301415285));
#137807=CARTESIAN_POINT('Ctrl Pts',(21.2841129263194,18.9711200467996,2.17872178885592));
#137808=CARTESIAN_POINT('Ctrl Pts',(21.2748827772654,18.8876278129311,2.18290056355899));
#137809=CARTESIAN_POINT('Ctrl Pts',(21.2615521105228,18.8046992141384,2.18707933826206));
#137810=CARTESIAN_POINT('Ctrl Pts',(21.248237345914,18.7218695407559,2.19125312811061));
#137811=CARTESIAN_POINT('Ctrl Pts',(21.2308318605463,18.6396026176039,2.19542691795915));
#137812=CARTESIAN_POINT('Ctrl Pts',(21.2094035421096,18.5583306321642,2.1996007078077));
#137813=CARTESIAN_POINT('Ctrl Pts',(21.1879892259254,18.4771117535917,2.20377177030927));
#137814=CARTESIAN_POINT('Ctrl Pts',(21.162557413063,18.3968869653703,2.20794283281085));
#137815=CARTESIAN_POINT('Ctrl Pts',(21.1332269868703,18.3180779062689,2.21211389531242));
#137816=CARTESIAN_POINT('Ctrl Pts',(21.1039069279456,18.2392967033815,2.21628348349098));
#137817=CARTESIAN_POINT('Ctrl Pts',(21.0706911534652,18.1619306662444,2.22045307166954));
#137818=CARTESIAN_POINT('Ctrl Pts',(21.0337478604524,18.0863846087019,2.2246226598481));
#137819=CARTESIAN_POINT('Ctrl Pts',(20.9968065436247,18.0108425922986,2.22879202498541));
#137820=CARTESIAN_POINT('Ctrl Pts',(20.9561383080875,17.93712077445,2.23296139012273));
#137821=CARTESIAN_POINT('Ctrl Pts',(20.9119581930928,17.8656011338119,2.23713075526004));
#137822=CARTESIAN_POINT('Ctrl Pts',(20.8677415457808,17.794022353939,2.24130356802463));
#137823=CARTESIAN_POINT('Ctrl Pts',(20.8200074610593,17.7246497803965,2.24547638078923));
#137824=CARTESIAN_POINT('Ctrl Pts',(20.7690150632332,17.657837518991,2.24964919355382));
#137825=CARTESIAN_POINT('Ctrl Pts',(20.7180006960884,17.5909964725131,2.25382380411293));
#137826=CARTESIAN_POINT('Ctrl Pts',(20.6637255153181,17.5267182882163,2.25799841467205));
#137827=CARTESIAN_POINT('Ctrl Pts',(20.6064883375299,17.4653232184008,2.26217302523117));
#137828=CARTESIAN_POINT('Ctrl Pts',(20.549164702276,17.4038354105723,2.26635394159121));
#137829=CARTESIAN_POINT('Ctrl Pts',(20.4888704631805,17.3452397372343,2.27053485795125));
#137830=CARTESIAN_POINT('Ctrl Pts',(20.4259403387529,17.2898186212383,2.2747157743113));
#137831=CARTESIAN_POINT('Ctrl Pts',(20.3829942581873,17.2519969939294,2.27756900195815));
#137832=CARTESIAN_POINT('Ctrl Pts',(20.3388212989463,17.2156530150771,2.280422229605));
#137833=CARTESIAN_POINT('Ctrl Pts',(20.2935357313021,17.1808649545431,2.28327545725186));
#137834=CARTESIAN_POINT('Origin',(18.734,19.211,-1.76670989022852));
#137835=CARTESIAN_POINT('',(20.2935357313021,17.1808649545432,3.14981136862994));
#137836=CARTESIAN_POINT('',(20.2933493626094,17.1811161618322,3.08342410898731));
#137837=CARTESIAN_POINT('',(20.2935357313021,17.1808649545432,-1.76670989022852));
#137838=CARTESIAN_POINT('',(16.1740010149448,19.2132795868243,2.63329010980609));
#137839=CARTESIAN_POINT('Ctrl Pts',(16.1740010149447,19.2132795868243,2.63329010980609));
#137840=CARTESIAN_POINT('Ctrl Pts',(16.1740928743929,19.3164386732002,2.6384134288319));
#137841=CARTESIAN_POINT('Ctrl Pts',(16.1804238944875,19.4193213099348,2.64353674785771));
#137842=CARTESIAN_POINT('Ctrl Pts',(16.1928719236876,19.5212710102101,2.64866006688352));
#137843=CARTESIAN_POINT('Ctrl Pts',(16.2055250386105,19.6249003681759,2.65386779441843));
#137844=CARTESIAN_POINT('Ctrl Pts',(16.2244983314989,19.7275658814857,2.65907552195333));
#137845=CARTESIAN_POINT('Ctrl Pts',(16.2496149571641,19.8286009706384,2.66428324948824));
#137846=CARTESIAN_POINT('Ctrl Pts',(16.2576437833531,19.8608980307853,2.66594796113282));
#137847=CARTESIAN_POINT('Ctrl Pts',(16.2662999939973,19.8930286552691,2.6676126727774));
#137848=CARTESIAN_POINT('Ctrl Pts',(16.2755767948953,19.9249715292663,2.66927738442198));
#137849=CARTESIAN_POINT('Ctrl Pts',(16.2988961609903,20.0052672671023,2.67346201883521));
#137850=CARTESIAN_POINT('Ctrl Pts',(16.3261969265522,20.084568763058,2.67764665324844));
#137851=CARTESIAN_POINT('Ctrl Pts',(16.3573766633344,20.1624523191503,2.68183128766167));
#137852=CARTESIAN_POINT('Ctrl Pts',(16.3885120196228,20.240225017646,2.68600996576606));
#137853=CARTESIAN_POINT('Ctrl Pts',(16.4235152107072,20.3165833617541,2.69018864387045));
#137854=CARTESIAN_POINT('Ctrl Pts',(16.4622338002162,20.391117932039,2.69436732197484));
#137855=CARTESIAN_POINT('Ctrl Pts',(16.5016463923758,20.4669884804673,2.6986208998552));
#137856=CARTESIAN_POINT('Ctrl Pts',(16.5449087556001,20.5409687666981,2.70287447773556));
#137857=CARTESIAN_POINT('Ctrl Pts',(16.5918084260801,20.6126473381798,2.70712805561591));
#137858=CARTESIAN_POINT('Ctrl Pts',(16.6377988552167,20.6829362811212,2.71129916961483));
#137859=CARTESIAN_POINT('Ctrl Pts',(16.687286554129,20.751011556649,2.71547028361374));
#137860=CARTESIAN_POINT('Ctrl Pts',(16.7400252973105,20.8165107863339,2.71964139761265));
#137861=CARTESIAN_POINT('Ctrl Pts',(16.7927463434995,20.8819880371221,2.72381111195413));
#137862=CARTESIAN_POINT('Ctrl Pts',(16.8487159791041,20.9448906007937,2.72798082629561));
#137863=CARTESIAN_POINT('Ctrl Pts',(16.9076465125811,21.004887660639,2.73215054063709));
#137864=CARTESIAN_POINT('Ctrl Pts',(16.9665749490585,21.0648825855332,2.73632010660235));
#137865=CARTESIAN_POINT('Ctrl Pts',(17.0284637509526,21.1219718845683,2.74048967256761));
#137866=CARTESIAN_POINT('Ctrl Pts',(17.0929880053962,21.1758612250147,2.74465923853288));
#137867=CARTESIAN_POINT('Ctrl Pts',(17.1597808523044,21.2316452475883,2.74897540124709));
#137868=CARTESIAN_POINT('Ctrl Pts',(17.2293975200615,21.2839997657394,2.7532915639613));
#137869=CARTESIAN_POINT('Ctrl Pts',(17.3014414464079,21.3326446428491,2.75760772667551));
#137870=CARTESIAN_POINT('Ctrl Pts',(17.3711385501858,21.3797049187129,2.76178329088849));
#137871=CARTESIAN_POINT('Ctrl Pts',(17.4431067778014,21.4232933214559,2.76595885510147));
#137872=CARTESIAN_POINT('Ctrl Pts',(17.5169602827149,21.4632021060621,2.77013441931445));
#137873=CARTESIAN_POINT('Ctrl Pts',(17.5945439513518,21.5051265878347,2.77452088127928));
#137874=CARTESIAN_POINT('Ctrl Pts',(17.6742078257196,21.5429897170844,2.77890734324411));
#137875=CARTESIAN_POINT('Ctrl Pts',(17.7554809190361,21.5766078305986,2.78329380520893));
#137876=CARTESIAN_POINT('Ctrl Pts',(17.8367540123527,21.6102259441129,2.78768026717376));
#137877=CARTESIAN_POINT('Ctrl Pts',(17.9196357523206,21.639598919772,2.79206672913859));
#137878=CARTESIAN_POINT('Ctrl Pts',(18.0036392138267,21.6646041086574,2.79645319110342));
#137879=CARTESIAN_POINT('Ctrl Pts',(18.0837775523631,21.6884587719788,2.80063782549363));
#137880=CARTESIAN_POINT('Ctrl Pts',(18.1652349468392,21.7084275441979,2.80482245988383));
#137881=CARTESIAN_POINT('Ctrl Pts',(18.247599691841,21.7243672115755,2.80900709427403));
#137882=CARTESIAN_POINT('Ctrl Pts',(18.3298472008232,21.7402841908096,2.81318577235515));
#137883=CARTESIAN_POINT('Ctrl Pts',(18.4129990472136,21.7521833699231,2.81736445043626));
#137884=CARTESIAN_POINT('Ctrl Pts',(18.4966284631471,21.7599713128029,2.82154312851737));
#137885=CARTESIAN_POINT('Ctrl Pts',(18.5817568763298,21.7678988489684,2.82579670640352));
#137886=CARTESIAN_POINT('Ctrl Pts',(18.6673796862237,21.7715661738212,2.83005028428966));
#137887=CARTESIAN_POINT('Ctrl Pts',(18.7530359237116,21.7709292243358,2.83430386217581));
#137888=CARTESIAN_POINT('Ctrl Pts',(18.8370315478211,21.7703046233595,2.83847497615096));
#137889=CARTESIAN_POINT('Ctrl Pts',(18.921058833767,21.7655411558159,2.84264609012612));
#137890=CARTESIAN_POINT('Ctrl Pts',(19.0046798014456,21.7566497098166,2.84681720410127));
#137891=CARTESIAN_POINT('Ctrl Pts',(19.0882727093013,21.7477612474278,2.85098691841887));
#137892=CARTESIAN_POINT('Ctrl Pts',(19.1714591125977,21.7347476061797,2.85515663273647));
#137893=CARTESIAN_POINT('Ctrl Pts',(19.2538051248627,21.7176716243191,2.85932634705406));
#137894=CARTESIAN_POINT('Ctrl Pts',(19.3361482069038,21.7005962500951,2.86349591299536));
#137895=CARTESIAN_POINT('Ctrl Pts',(19.4176505070952,21.6794589169156,2.86766547893665));
#137896=CARTESIAN_POINT('Ctrl Pts',(19.4978886690214,21.654373508357,2.87183504487794));
#137897=CARTESIAN_POINT('Ctrl Pts',(19.5809479058551,21.6284061277425,2.87615120762019));
#137898=CARTESIAN_POINT('Ctrl Pts',(19.6626519528601,21.5982080349117,2.88046737036243));
#137899=CARTESIAN_POINT('Ctrl Pts',(19.7425506078302,21.5639610433336,2.88478353310467));
#137900=CARTESIAN_POINT('Ctrl Pts',(19.8198465724097,21.5308296439505,2.88895909729369));
#137901=CARTESIAN_POINT('Ctrl Pts',(19.8954525574108,21.4939093297994,2.89313466148271));
#137902=CARTESIAN_POINT('Ctrl Pts',(19.9689850307412,21.4534120883203,2.89731022567173));
#137903=CARTESIAN_POINT('Ctrl Pts',(20.0462314546531,21.4108694273588,2.90169668769058));
#137904=CARTESIAN_POINT('Ctrl Pts',(20.1211888996701,21.364379309383,2.90608314970944));
#137905=CARTESIAN_POINT('Ctrl Pts',(20.193447997866,21.3142383463424,2.91046961172829));
#137906=CARTESIAN_POINT('Ctrl Pts',(20.2657070960619,21.2640973833017,2.91485607374715));
#137907=CARTESIAN_POINT('Ctrl Pts',(20.3352674349797,21.2103059903068,2.919242535766));
#137908=CARTESIAN_POINT('Ctrl Pts',(20.401762322946,21.1532072068041,2.92362899778486));
#137909=CARTESIAN_POINT('Ctrl Pts',(20.4651976823984,21.0987356230994,2.92781363217407));
#137910=CARTESIAN_POINT('Ctrl Pts',(20.5260796023552,21.0410515629438,2.93199826656328));
#137911=CARTESIAN_POINT('Ctrl Pts',(20.584064814394,20.9804236865549,2.93618290095249));
#137912=CARTESIAN_POINT('Ctrl Pts',(20.6419674916594,20.919882106445,2.94036157903251));
#137913=CARTESIAN_POINT('Ctrl Pts',(20.6969813355446,20.8564053626881,2.94454025711254));
#137914=CARTESIAN_POINT('Ctrl Pts',(20.7487967797138,20.7903017243247,2.94871893519257));
#137915=CARTESIAN_POINT('Ctrl Pts',(20.8015409785421,20.723013225673,2.95297251307897));
#137916=CARTESIAN_POINT('Ctrl Pts',(20.8509706214137,20.6530030460431,2.95722609096538));
#137917=CARTESIAN_POINT('Ctrl Pts',(20.8967991444563,20.5806349370322,2.96147966885178));
#137918=CARTESIAN_POINT('Ctrl Pts',(20.9417391920986,20.5096698251147,2.96565078282566));
#137919=CARTESIAN_POINT('Ctrl Pts',(20.9832162459024,20.4364378006298,2.96982189679954));
#137920=CARTESIAN_POINT('Ctrl Pts',(21.021002390723,20.361313029061,2.97399301077341));
#137921=CARTESIAN_POINT('Ctrl Pts',(21.0587758560373,20.2862134663357,2.97816272508966));
#137922=CARTESIAN_POINT('Ctrl Pts',(21.0928606655495,20.2092228285369,2.98233243940591));
#137923=CARTESIAN_POINT('Ctrl Pts',(21.1230748017628,20.1307399586743,2.98650215372215));
#137924=CARTESIAN_POINT('Ctrl Pts',(21.153287862827,20.0522598815699,2.99067171966203));
#137925=CARTESIAN_POINT('Ctrl Pts',(21.1796303599629,19.972288107602,2.9948412856019));
#137926=CARTESIAN_POINT('Ctrl Pts',(21.2019688964371,19.8912422555377,2.99901085154177));
#137927=CARTESIAN_POINT('Ctrl Pts',(21.2250928283449,19.8073469311187,3.00332701428548));
#137928=CARTESIAN_POINT('Ctrl Pts',(21.2439258622492,19.7223011025982,3.00764317702919));
#137929=CARTESIAN_POINT('Ctrl Pts',(21.2583771885884,19.6365817309687,3.0119593397729));
#137930=CARTESIAN_POINT('Ctrl Pts',(21.2723577644625,19.5536546590302,3.01613490396034));
#137931=CARTESIAN_POINT('Ctrl Pts',(21.2822377087348,19.4700977247691,3.02031046814778));
#137932=CARTESIAN_POINT('Ctrl Pts',(21.2879876706469,19.3863481627603,3.02448603233521));
#137933=CARTESIAN_POINT('Ctrl Pts',(21.294028049485,19.2983686091941,3.02887249435706));
#137934=CARTESIAN_POINT('Ctrl Pts',(21.295510260803,19.2101770410253,3.03325895637891));
#137935=CARTESIAN_POINT('Ctrl Pts',(21.2924621252161,19.1222782223196,3.03764541840075));
#137936=CARTESIAN_POINT('Ctrl Pts',(21.2894139896292,19.034379403614,3.0420318804226));
#137937=CARTESIAN_POINT('Ctrl Pts',(21.2818356329245,18.9467739058741,3.04641834244444));
#137938=CARTESIAN_POINT('Ctrl Pts',(21.2698170137414,18.859955739515,3.05080480446629));
#137939=CARTESIAN_POINT('Ctrl Pts',(21.2583547009868,18.7771561299731,3.0549882301007));
#137940=CARTESIAN_POINT('Ctrl Pts',(21.2428114366921,18.6947644704986,3.0591716557351));
#137941=CARTESIAN_POINT('Ctrl Pts',(21.223227274647,18.6132144404944,3.06335508136951));
#137942=CARTESIAN_POINT('Ctrl Pts',(21.2036685685073,18.5317704109331,3.06753306929936));
#137943=CARTESIAN_POINT('Ctrl Pts',(21.1800794975097,18.451166282156,3.07171105722921));
#137944=CARTESIAN_POINT('Ctrl Pts',(21.1525516402429,18.3718290022419,3.07588904515905));
#137945=CARTESIAN_POINT('Ctrl Pts',(21.1250513038495,18.2925710394797,3.08006285616094));
#137946=CARTESIAN_POINT('Ctrl Pts',(21.0936201503635,18.2145778427157,3.08423666716283));
#137947=CARTESIAN_POINT('Ctrl Pts',(21.0584001058549,18.1382632438935,3.08841047816471));
#137948=CARTESIAN_POINT('Ctrl Pts',(21.0232047055557,18.0620020440089,3.09258136866283));
#137949=CARTESIAN_POINT('Ctrl Pts',(20.984225873128,17.9874175251834,3.09675225916096));
#137950=CARTESIAN_POINT('Ctrl Pts',(20.9416538964403,17.9149042189978,3.10092314965908));
#137951=CARTESIAN_POINT('Ctrl Pts',(20.8990871157843,17.8423997632687,3.10509353108808));
#137952=CARTESIAN_POINT('Ctrl Pts',(20.8529282822876,17.7719664217416,3.10926391251708));
#137953=CARTESIAN_POINT('Ctrl Pts',(20.8034134872375,17.7039738493179,3.11343429394608));
#137954=CARTESIAN_POINT('Ctrl Pts',(20.7539049126747,17.6359898187238,3.11760415145481));
#137955=CARTESIAN_POINT('Ctrl Pts',(20.7010414902565,17.5704463163578,3.12177400896353));
#137956=CARTESIAN_POINT('Ctrl Pts',(20.6451014451984,17.5076822768019,3.12594386647225));
#137957=CARTESIAN_POINT('Ctrl Pts',(20.589118959079,17.4448706188996,3.13011688760334));
#137958=CARTESIAN_POINT('Ctrl Pts',(20.5300554962174,17.3848429785817,3.13428990873442));
#137959=CARTESIAN_POINT('Ctrl Pts',(20.4682278066193,17.3279031053214,3.13846292986551));
#137960=CARTESIAN_POINT('Ctrl Pts',(20.412181461353,17.2762875295669,3.14224574278699));
#137961=CARTESIAN_POINT('Ctrl Pts',(20.3538643315057,17.2272089688724,3.14602855570846));
#137962=CARTESIAN_POINT('Ctrl Pts',(20.2935357313021,17.1808649545431,3.14981136862994));
#137963=CARTESIAN_POINT('Ctrl Pts',(20.2935357313021,17.1808649545431,2.34989189381266));
#137964=CARTESIAN_POINT('Ctrl Pts',(20.2268473226505,17.1296353792553,2.35406143415155));
#137965=CARTESIAN_POINT('Ctrl Pts',(20.157629382282,17.0816932397055,2.35823097449044));
#137966=CARTESIAN_POINT('Ctrl Pts',(20.086244262461,17.0372853327446,2.36240051482933));
#137967=CARTESIAN_POINT('Ctrl Pts',(20.0113055121266,16.9906667508754,2.36677761951515));
#137968=CARTESIAN_POINT('Ctrl Pts',(19.9339786728819,16.9479437267017,2.37115472420096));
#137969=CARTESIAN_POINT('Ctrl Pts',(19.8547138818835,16.9093483332716,2.37553182888678));
#137970=CARTESIAN_POINT('Ctrl Pts',(19.779100692075,16.8725309674222,2.37970728741321));
#137971=CARTESIAN_POINT('Ctrl Pts',(19.7017246208009,16.8394694658615,2.38388274593965));
#137972=CARTESIAN_POINT('Ctrl Pts',(19.6229967480141,16.8103157679486,2.38805820446608));
#137973=CARTESIAN_POINT('Ctrl Pts',(19.5442131803373,16.7811414456755,2.39223661686));
#137974=CARTESIAN_POINT('Ctrl Pts',(19.4640763462349,16.75588056566,2.39641502925392));
#137975=CARTESIAN_POINT('Ctrl Pts',(19.3830113793374,16.7346348755705,2.40059344164783));
#137976=CARTESIAN_POINT('Ctrl Pts',(19.301820161026,16.7133560972246,2.40477836154422));
#137977=CARTESIAN_POINT('Ctrl Pts',(19.2196983754079,16.6961050747908,2.40896328144061));
#137978=CARTESIAN_POINT('Ctrl Pts',(19.1370795418308,16.682932183869,2.413148201337));
#137979=CARTESIAN_POINT('Ctrl Pts',(19.1253819274855,16.6810670958358,2.41374072457771));
#137980=CARTESIAN_POINT('Ctrl Pts',(19.1136743529045,16.6792836744105,2.41433324781841));
#137981=CARTESIAN_POINT('Ctrl Pts',(19.1019580505852,16.6775819782338,2.41492577105911));
#137982=CARTESIAN_POINT('Ctrl Pts',(19.0192128717126,16.6655639241852,2.41911040544304));
#137983=CARTESIAN_POINT('Ctrl Pts',(18.9357242972397,16.6575816378624,2.42329503982696));
#137984=CARTESIAN_POINT('Ctrl Pts',(18.8519204122533,16.6537173061286,2.42747967421088));
#137985=CARTESIAN_POINT('Ctrl Pts',(18.7682358117202,16.6498584747926,2.43165835228592));
#137986=CARTESIAN_POINT('Ctrl Pts',(18.6842372477564,16.6501059764731,2.43583703036095));
#137987=CARTESIAN_POINT('Ctrl Pts',(18.6003605130585,16.6544905657264,2.44001570843599));
#137988=CARTESIAN_POINT('Ctrl Pts',(18.514980347945,16.6589537456027,2.44426928632368));
#137989=CARTESIAN_POINT('Ctrl Pts',(18.4297268997694,16.6677038557791,2.44852286421137));
#137990=CARTESIAN_POINT('Ctrl Pts',(18.3450626650523,16.6807178518031,2.45277644209906));
#137991=CARTESIAN_POINT('Ctrl Pts',(18.2620398119427,16.6934795460874,2.45694755606873));
#137992=CARTESIAN_POINT('Ctrl Pts',(18.1795840056908,16.7103412009465,2.4611186700384));
#137993=CARTESIAN_POINT('Ctrl Pts',(18.0981270507744,16.7312287217481,2.46528978400808));
#137994=CARTESIAN_POINT('Ctrl Pts',(18.016697429521,16.7521092335416,2.46945949832042));
#137995=CARTESIAN_POINT('Ctrl Pts',(17.9362664391868,16.7770128141615,2.47362921263276));
#137996=CARTESIAN_POINT('Ctrl Pts',(17.857254322942,16.8058145564718,2.4777989269451));
#137997=CARTESIAN_POINT('Ctrl Pts',(17.7782450182824,16.8346152738942,2.48196849288137));
#137998=CARTESIAN_POINT('Ctrl Pts',(17.700654919247,16.8673137188575,2.48613805881764));
#137999=CARTESIAN_POINT('Ctrl Pts',(17.6248864697081,16.9037359975669,2.49030762475391));
#138000=CARTESIAN_POINT('Ctrl Pts',(17.5464540946267,16.9414388388213,2.4946237875028));
#138001=CARTESIAN_POINT('Ctrl Pts',(17.469974326197,16.9831320174923,2.49893995025168));
#138002=CARTESIAN_POINT('Ctrl Pts',(17.3958663510851,17.0285705423446,2.50325611300057));
#138003=CARTESIAN_POINT('Ctrl Pts',(17.3241724357538,17.0725289118538,2.50743167718523));
#138004=CARTESIAN_POINT('Ctrl Pts',(17.2546985266634,17.1199920607125,2.51160724136989));
#138005=CARTESIAN_POINT('Ctrl Pts',(17.1877934784103,17.1706947795505,2.51578280555456));
#138006=CARTESIAN_POINT('Ctrl Pts',(17.1175092148078,17.2239583724964,2.52016926758556));
#138007=CARTESIAN_POINT('Ctrl Pts',(17.0500605848375,17.2807970211555,2.52455572961656));
#138008=CARTESIAN_POINT('Ctrl Pts',(16.9858097729218,17.3408580455087,2.52894219164756));
#138009=CARTESIAN_POINT('Ctrl Pts',(16.9215589610062,17.400919069862,2.53332865367856));
#138010=CARTESIAN_POINT('Ctrl Pts',(16.8605063152545,17.464201999529,2.53771511570955));
#138011=CARTESIAN_POINT('Ctrl Pts',(16.802965079949,17.53031438468,2.54210157774055));
#138012=CARTESIAN_POINT('Ctrl Pts',(16.7485317522924,17.5928559186595,2.54625111891253));
#138013=CARTESIAN_POINT('Ctrl Pts',(16.6970294692197,17.6581717364498,2.55040066008451));
#138014=CARTESIAN_POINT('Ctrl Pts',(16.6487573722079,17.7259534743858,2.55455020125649));
#138015=CARTESIAN_POINT('Ctrl Pts',(16.600549374283,17.7936452069609,2.55869423237573));
#138016=CARTESIAN_POINT('Ctrl Pts',(16.5555633203294,17.8637959851695,2.56283826349497));
#138017=CARTESIAN_POINT('Ctrl Pts',(16.5140597201748,17.9360626862432,2.56698229461421));
#138018=CARTESIAN_POINT('Ctrl Pts',(16.4725982721945,18.0082559913085,2.57112211694382));
#138019=CARTESIAN_POINT('Ctrl Pts',(16.4346124893249,18.0825605501313,2.57526193927342));
#138020=CARTESIAN_POINT('Ctrl Pts',(16.4003201033264,18.1586036203684,2.57940176160303));
#138021=CARTESIAN_POINT('Ctrl Pts',(16.3660518421391,18.2345931940449,2.58353867155343));
#138022=CARTESIAN_POINT('Ctrl Pts',(16.3354720095434,18.3123184246929,2.58767558150382));
#138023=CARTESIAN_POINT('Ctrl Pts',(16.3087521158413,18.3913825890187,2.59181249145422));
#138024=CARTESIAN_POINT('Ctrl Pts',(16.2820372325134,18.4704319276473,2.59594862567298));
#138025=CARTESIAN_POINT('Ctrl Pts',(16.2591810094474,18.5508192612106,2.60008475989173));
#138026=CARTESIAN_POINT('Ctrl Pts',(16.2403061251843,18.6321296702138,2.60422089411049));
#138027=CARTESIAN_POINT('Ctrl Pts',(16.2214331728159,18.7134317568803,2.6083566049849));
#138028=CARTESIAN_POINT('Ctrl Pts',(16.2065408484307,18.7956562735366,2.61249231585931));
#138029=CARTESIAN_POINT('Ctrl Pts',(16.1957010120579,18.878376717874,2.61662802673372));
#138030=CARTESIAN_POINT('Ctrl Pts',(16.1848552750843,18.9611421905962,2.62076598885789));
#138031=CARTESIAN_POINT('Ctrl Pts',(16.1780664813585,19.0444036643639,2.62490395098206));
#138032=CARTESIAN_POINT('Ctrl Pts',(16.175354661978,19.1277291514511,2.62904191310623));
#138033=CARTESIAN_POINT('Ctrl Pts',(16.1744266413965,19.1562442389712,2.63045797866132));
#138034=CARTESIAN_POINT('Ctrl Pts',(16.1739756253558,19.1847668138065,2.63187404421641));
#138035=CARTESIAN_POINT('Ctrl Pts',(16.1740010149441,19.213279586128,2.6332901097715));
#138036=CARTESIAN_POINT('',(16.1740009418753,19.2088040034395,2.56670989022851));
#138037=CARTESIAN_POINT('Ctrl Pts',(20.2935357313021,17.1808649545431,2.28327545725186));
#138038=CARTESIAN_POINT('Ctrl Pts',(20.2623792546742,17.1569307642185,2.28523847825651));
#138039=CARTESIAN_POINT('Ctrl Pts',(20.2306962622582,17.1337328627522,2.28720149926116));
#138040=CARTESIAN_POINT('Ctrl Pts',(20.1985254700647,17.1112940330771,2.28916452026581));
#138041=CARTESIAN_POINT('Ctrl Pts',(20.1299459675149,17.0634604650486,2.29334915467531));
#138042=CARTESIAN_POINT('Ctrl Pts',(20.0588929044646,17.0189012759396,2.2975337890848));
#138043=CARTESIAN_POINT('Ctrl Pts',(19.9857121094414,16.9778818224111,2.3017184234943));
#138044=CARTESIAN_POINT('Ctrl Pts',(19.9126354781723,16.9369207549698,2.30589710159751));
#138045=CARTESIAN_POINT('Ctrl Pts',(19.8374375284665,16.8994896383239,2.31007577970071));
#138046=CARTESIAN_POINT('Ctrl Pts',(19.7604940332793,16.8658113083076,2.31425445780392));
#138047=CARTESIAN_POINT('Ctrl Pts',(19.6821713816824,16.8315293186239,2.31850803568489));
#138048=CARTESIAN_POINT('Ctrl Pts',(19.6020403867561,16.8011362520523,2.32276161356587));
#138049=CARTESIAN_POINT('Ctrl Pts',(19.5205248076185,16.7748188230346,2.32701519144684));
#138050=CARTESIAN_POINT('Ctrl Pts',(19.4405895664632,16.7490116085441,2.33118630545089));
#138051=CARTESIAN_POINT('Ctrl Pts',(19.3593234056723,16.7271235613564,2.33535741945494));
#138052=CARTESIAN_POINT('Ctrl Pts',(19.2771455317487,16.7092820040337,2.33952853345898));
#138053=CARTESIAN_POINT('Ctrl Pts',(19.1949952333547,16.6914464336072,2.34369824780796));
#138054=CARTESIAN_POINT('Ctrl Pts',(19.1119342786025,16.6776547538833,2.34786796215693));
#138055=CARTESIAN_POINT('Ctrl Pts',(19.0283943159519,16.6679836833525,2.3520376765059));
#138056=CARTESIAN_POINT('Ctrl Pts',(18.9448573259619,16.6583129569542,2.35620724248102));
#138057=CARTESIAN_POINT('Ctrl Pts',(18.8608418190422,16.6527626002741,2.36037680845614));
#138058=CARTESIAN_POINT('Ctrl Pts',(18.7767854909837,16.6513575636896,2.36454637443126));
#138059=CARTESIAN_POINT('Ctrl Pts',(18.6897738473637,16.6499031277727,2.36886253714093));
#138060=CARTESIAN_POINT('Ctrl Pts',(18.602718986005,16.6528909431625,2.3731786998506));
#138061=CARTESIAN_POINT('Ctrl Pts',(18.516105438621,16.6602899106089,2.37749486256026));
#138062=CARTESIAN_POINT('Ctrl Pts',(18.4323133171228,16.6674478575809,2.38167042678893));
#138063=CARTESIAN_POINT('Ctrl Pts',(18.3489346599913,16.6787338735485,2.3858459910176));
#138064=CARTESIAN_POINT('Ctrl Pts',(18.2664001913304,16.694067259752,2.39002155524626));
#138065=CARTESIAN_POINT('Ctrl Pts',(18.1796971048655,16.7101750984693,2.39440801719643));
#138066=CARTESIAN_POINT('Ctrl Pts',(18.0939262957202,16.7307497815375,2.39879447914659));
#138067=CARTESIAN_POINT('Ctrl Pts',(18.0095696123178,16.7556383945735,2.40318094109676));
#138068=CARTESIAN_POINT('Ctrl Pts',(17.9252129289154,16.7805270076095,2.40756740304692));
#138069=CARTESIAN_POINT('Ctrl Pts',(17.8422708932813,16.8097292861762,2.41195386499709));
#138070=CARTESIAN_POINT('Ctrl Pts',(17.7611994326656,16.8430348279179,2.41634032694725));
#138071=CARTESIAN_POINT('Ctrl Pts',(17.6838581936306,16.8748079308751,2.42052496109137));
#138072=CARTESIAN_POINT('Ctrl Pts',(17.6079312972171,16.9104332654877,2.42470959523549));
#138073=CARTESIAN_POINT('Ctrl Pts',(17.5338290567806,16.9497636773101,2.4288942293796));
#138074=CARTESIAN_POINT('Ctrl Pts',(17.4598322917951,16.9890381071151,2.43307290721024));
#138075=CARTESIAN_POINT('Ctrl Pts',(17.3876554268513,17.0320069250301,2.43725158504088));
#138076=CARTESIAN_POINT('Ctrl Pts',(17.3176892303787,17.0784747823637,2.44143026287152));
#138077=CARTESIAN_POINT('Ctrl Pts',(17.2464689347497,17.1257755462096,2.44568384081973));
#138078=CARTESIAN_POINT('Ctrl Pts',(17.1775397858983,17.1767018411992,2.44993741876795));
#138079=CARTESIAN_POINT('Ctrl Pts',(17.1112881539821,17.2309984179822,2.45419099671616));
#138080=CARTESIAN_POINT('Ctrl Pts',(17.046320944273,17.2842423455401,2.45836211043189));
#138081=CARTESIAN_POINT('Ctrl Pts',(16.9839287319629,17.3407267365349,2.46253322414762));
#138082=CARTESIAN_POINT('Ctrl Pts',(16.9244454837024,17.4001680220001,2.46670433786335));
#138083=CARTESIAN_POINT('Ctrl Pts',(16.864982195661,17.4595893613273,2.47087405191874));
#138084=CARTESIAN_POINT('Ctrl Pts',(16.80842625819,17.5219652996602,2.47504376597413));
#138085=CARTESIAN_POINT('Ctrl Pts',(16.7550758225251,17.5869744152861,2.47921348002952));
#138086=CARTESIAN_POINT('Ctrl Pts',(16.7017272853287,17.6519812175709,2.48338304570617));
#138087=CARTESIAN_POINT('Ctrl Pts',(16.6515843143223,17.7196206546924,2.48755261138281));
#138088=CARTESIAN_POINT('Ctrl Pts',(16.6049048052609,17.789538198987,2.49172217705945));
#138089=CARTESIAN_POINT('Ctrl Pts',(16.5565840956936,17.8619139677013,2.49603834010689));
#138090=CARTESIAN_POINT('Ctrl Pts',(16.5119752240704,17.9367305827085,2.50035450315433));
#138091=CARTESIAN_POINT('Ctrl Pts',(16.4713143087829,18.0135637959534,2.50467066620176));
#138092=CARTESIAN_POINT('Ctrl Pts',(16.4319779238963,18.087894165226,2.50884623012272));
#138093=CARTESIAN_POINT('Ctrl Pts',(16.3963363916594,18.1641113217507,2.51302179404367));
#138094=CARTESIAN_POINT('Ctrl Pts',(16.3645549999772,18.241809414064,2.51719735796462));
#138095=CARTESIAN_POINT('Ctrl Pts',(16.331168399037,18.3234318687324,2.5215838205753));
#138096=CARTESIAN_POINT('Ctrl Pts',(16.3020423326827,18.4066882445185,2.52597028318598));
#138097=CARTESIAN_POINT('Ctrl Pts',(16.2773090396161,18.491090613224,2.53035674579666));
#138098=CARTESIAN_POINT('Ctrl Pts',(16.2525757465496,18.5754929819294,2.53474320840733));
#138099=CARTESIAN_POINT('Ctrl Pts',(16.2322352869838,18.6610407614778,2.53912967101801));
#138100=CARTESIAN_POINT('Ctrl Pts',(16.2163575306379,18.7472367021162,2.54351613362869));
#138101=CARTESIAN_POINT('Ctrl Pts',(16.1935441105101,18.8710844400618,2.54981867488401));
#138102=CARTESIAN_POINT('Ctrl Pts',(16.179864182312,18.9966631544576,2.55612121613934));
#138103=CARTESIAN_POINT('Ctrl Pts',(16.1755170133968,19.1228818562274,2.56242375739466));
#138104=CARTESIAN_POINT('Ctrl Pts',(16.1745315620438,19.1514941307573,2.56385246833928));
#138105=CARTESIAN_POINT('Ctrl Pts',(16.1740255308992,19.180139168944,2.56528117928389));
#138106=CARTESIAN_POINT('Ctrl Pts',(16.1740009418753,19.2088040034395,2.56670989022851));
#138107=CARTESIAN_POINT('Ctrl Pts',(16.17268506744,19.2088155460777,2.56671052147119));
#138108=CARTESIAN_POINT('Ctrl Pts',(16.1790130470455,19.904586810716,2.60137099441749));
#138109=CARTESIAN_POINT('Ctrl Pts',(16.8320815026504,21.4617759084344,2.67842340292429));
#138110=CARTESIAN_POINT('Ctrl Pts',(19.467398376245,22.1479063348824,2.79786774699155));
#138111=CARTESIAN_POINT('Ctrl Pts',(21.6004480826227,20.1840197191269,2.92504355367299));
#138112=CARTESIAN_POINT('Ctrl Pts',(21.2286613330159,18.0460023426628,3.02022900767158));
#138113=CARTESIAN_POINT('Ctrl Pts',(20.4604812953147,17.3068568960671,3.07302252610969));
#138114=CARTESIAN_POINT('Ctrl Pts',(20.2933493626091,17.181116161832,3.08342410898733));
#138115=CARTESIAN_POINT('Origin',(18.734,19.211,-1.76670989022852));
#138116=CARTESIAN_POINT('',(20.2935357313021,17.1808649545431,3.9499316895625));
#138117=CARTESIAN_POINT('',(20.2935357313021,17.1808649545432,3.88329345306099));
#138118=CARTESIAN_POINT('',(20.2935357313021,17.1808649545432,-1.76670989022852));
#138119=CARTESIAN_POINT('',(16.1740000028035,19.2108801919503,3.43329010980363));
#138120=CARTESIAN_POINT('Ctrl Pts',(16.1740000028035,19.2108801919503,3.43329010980363));
#138121=CARTESIAN_POINT('Ctrl Pts',(16.173996094898,19.2943824116246,3.43746913841142));
#138122=CARTESIAN_POINT('Ctrl Pts',(16.1780820066338,19.3780422026732,3.4416481670192));
#138123=CARTESIAN_POINT('Ctrl Pts',(16.1862780259001,19.4614251239166,3.44582719562699));
#138124=CARTESIAN_POINT('Ctrl Pts',(16.1944623792895,19.5446893613378,3.45000027597725));
#138125=CARTESIAN_POINT('Ctrl Pts',(16.2067451760218,19.6276770564327,3.45417335632751));
#138126=CARTESIAN_POINT('Ctrl Pts',(16.2230946976723,19.7099534675123,3.45834643667778));
#138127=CARTESIAN_POINT('Ctrl Pts',(16.2396087147061,19.7930576758859,3.46256150311587));
#138128=CARTESIAN_POINT('Ctrl Pts',(16.2602717621694,19.8754357285734,3.46677656955397));
#138129=CARTESIAN_POINT('Ctrl Pts',(16.2849973159137,19.9566445891563,3.47099163599206));
#138130=CARTESIAN_POINT('Ctrl Pts',(16.3094325809408,20.0369000225196,3.47515721572334));
#138131=CARTESIAN_POINT('Ctrl Pts',(16.3378353258574,20.1160131199902,3.47932279545462));
#138132=CARTESIAN_POINT('Ctrl Pts',(16.3700710228283,20.1935679573893,3.4834883751859));
#138133=CARTESIAN_POINT('Ctrl Pts',(16.4022960455082,20.2710971138511,3.48765257555782));
#138134=CARTESIAN_POINT('Ctrl Pts',(16.4383513227395,20.3470686092118,3.49181677592973));
#138135=CARTESIAN_POINT('Ctrl Pts',(16.4780536821042,20.4210852080628,3.49598097630165));
#138136=CARTESIAN_POINT('Ctrl Pts',(16.5177548909312,20.495099661981,3.50014505599888));
#138137=CARTESIAN_POINT('Ctrl Pts',(16.561102752779,20.5671589258651,3.50430913569611));
#138138=CARTESIAN_POINT('Ctrl Pts',(16.6078681568273,20.636890383391,3.50847321539335));
#138139=CARTESIAN_POINT('Ctrl Pts',(16.6556310871523,20.7081092430383,3.5127261167099));
#138140=CARTESIAN_POINT('Ctrl Pts',(16.7069587733461,20.7768994173764,3.51697901802646));
#138141=CARTESIAN_POINT('Ctrl Pts',(16.761561649075,20.8428967344168,3.52123191934301));
#138142=CARTESIAN_POINT('Ctrl Pts',(16.8151012611779,20.9076089076679,3.52540200532769));
#138143=CARTESIAN_POINT('Ctrl Pts',(16.8717892886061,20.9696357146529,3.52957209131237));
#138144=CARTESIAN_POINT('Ctrl Pts',(16.9313144499797,21.028670159228,3.53374217729704));
#138145=CARTESIAN_POINT('Ctrl Pts',(16.9926128107595,21.0894631852106,3.53803648627954));
#138146=CARTESIAN_POINT('Ctrl Pts',(17.0569196193486,21.1470823903912,3.54233079526204));
#138147=CARTESIAN_POINT('Ctrl Pts',(17.1238587796064,21.2012374859271,3.54662510424453));
#138148=CARTESIAN_POINT('Ctrl Pts',(17.1907979398641,21.255392581463,3.55091941322703));
#138149=CARTESIAN_POINT('Ctrl Pts',(17.2603689845985,21.3060833143331,3.55521372220952));
#138150=CARTESIAN_POINT('Ctrl Pts',(17.3321657913456,21.3530692919339,3.55950803119202));
#138151=CARTESIAN_POINT('Ctrl Pts',(17.4021289421207,21.3988552702266,3.56369266558496));
#138152=CARTESIAN_POINT('Ctrl Pts',(17.4744678068902,21.4412951999105,3.5678772999779));
#138153=CARTESIAN_POINT('Ctrl Pts',(17.5488288662329,21.4801340603158,3.57206193437084));
#138154=CARTESIAN_POINT('Ctrl Pts',(17.6230840818118,21.5189176384105,3.57624061245467));
#138155=CARTESIAN_POINT('Ctrl Pts',(17.6993553703912,21.5541101172787,3.58041929053851));
#138156=CARTESIAN_POINT('Ctrl Pts',(17.7772605377966,21.5854998634371,3.58459796862235));
#138157=CARTESIAN_POINT('Ctrl Pts',(17.8565620993408,21.6174522482369,3.58885154650781));
#138158=CARTESIAN_POINT('Ctrl Pts',(17.9375562869758,21.6454639674282,3.59310512439327));
#138159=CARTESIAN_POINT('Ctrl Pts',(18.0198140087909,21.6693609112497,3.59735870227874));
#138160=CARTESIAN_POINT('Ctrl Pts',(18.1004770041531,21.6927945661834,3.60152981625657));
#138161=CARTESIAN_POINT('Ctrl Pts',(18.1823545166283,21.7122714336376,3.60570093023441));
#138162=CARTESIAN_POINT('Ctrl Pts',(18.265023760118,21.7276766352526,3.60987204421225));
#138163=CARTESIAN_POINT('Ctrl Pts',(18.3476652631446,21.7430766675033,3.6140417585325));
#138164=CARTESIAN_POINT('Ctrl Pts',(18.4310975176837,21.754407663177,3.61821147285276));
#138165=CARTESIAN_POINT('Ctrl Pts',(18.5148867965887,21.7616056935737,3.62238118717302));
#138166=CARTESIAN_POINT('Ctrl Pts',(18.5986730939115,21.7688034678337,3.62655075311695));
#138167=CARTESIAN_POINT('Ctrl Pts',(18.682815931923,21.7718685307012,3.63072031906087));
#138168=CARTESIAN_POINT('Ctrl Pts',(18.7668770686623,21.7707888776921,3.6348898850048));
#138169=CARTESIAN_POINT('Ctrl Pts',(18.8538936912739,21.769671265415,3.63920604774385));
#138170=CARTESIAN_POINT('Ctrl Pts',(18.9408222331038,21.7641120647909,3.64352221048291));
#138171=CARTESIAN_POINT('Ctrl Pts',(19.0271792931093,21.7541566806023,3.64783837322197));
#138172=CARTESIAN_POINT('Ctrl Pts',(19.1107232809634,21.744525592007,3.65201393741353));
#138173=CARTESIAN_POINT('Ctrl Pts',(19.1937319902683,21.730780456376,3.6561895016051));
#138174=CARTESIAN_POINT('Ctrl Pts',(19.2757772698989,21.7130146661882,3.66036506579667));
#138175=CARTESIAN_POINT('Ctrl Pts',(19.3619664615668,21.6943515681706,3.66475152780947));
#138176=CARTESIAN_POINT('Ctrl Pts',(19.4470917766266,21.6712511277376,3.66913798982227));
#138177=CARTESIAN_POINT('Ctrl Pts',(19.5306760960811,21.6438804323133,3.67352445183507));
#138178=CARTESIAN_POINT('Ctrl Pts',(19.6142604155355,21.616509736889,3.67791091384787));
#138179=CARTESIAN_POINT('Ctrl Pts',(19.6963032254017,21.584869066222,3.68229737586066));
#138180=CARTESIAN_POINT('Ctrl Pts',(19.7763550154477,21.5491822045707,3.68668383787346));
#138181=CARTESIAN_POINT('Ctrl Pts',(19.8527235039631,21.515137348327,3.69086847226646));
#138182=CARTESIAN_POINT('Ctrl Pts',(19.9275644240484,21.4772837399298,3.69505310665946));
#138183=CARTESIAN_POINT('Ctrl Pts',(20.0004719903204,21.4357805954147,3.69923774105245));
#138184=CARTESIAN_POINT('Ctrl Pts',(20.0732757816959,21.3943365254888,3.70341641913635));
#138185=CARTESIAN_POINT('Ctrl Pts',(20.1441512890029,21.3492534633191,3.70759509722024));
#138186=CARTESIAN_POINT('Ctrl Pts',(20.2127136875159,21.3007382205322,3.71177377530413));
#138187=CARTESIAN_POINT('Ctrl Pts',(20.2825050177484,21.2513533768849,3.71602735318958));
#138188=CARTESIAN_POINT('Ctrl Pts',(20.3498990582276,21.1984122950061,3.72028093107503));
#138189=CARTESIAN_POINT('Ctrl Pts',(20.4145171508851,21.1421815309755,3.72453450896047));
#138190=CARTESIAN_POINT('Ctrl Pts',(20.4778824957237,21.0870409100319,3.72870562293838));
#138191=CARTESIAN_POINT('Ctrl Pts',(20.5385782035452,21.0287373383814,3.73287673691628));
#138192=CARTESIAN_POINT('Ctrl Pts',(20.5962788337327,20.9675641307482,3.73704785089418));
#138193=CARTESIAN_POINT('Ctrl Pts',(20.6539601019164,20.9064114503757,3.7412175652145));
#138194=CARTESIAN_POINT('Ctrl Pts',(20.7086479730736,20.8423913807966,3.74538727953482));
#138195=CARTESIAN_POINT('Ctrl Pts',(20.7600539250066,20.7758340145094,3.74955699385514));
#138196=CARTESIAN_POINT('Ctrl Pts',(20.811458047695,20.7092790166189,3.75372655979913));
#138197=CARTESIAN_POINT('Ctrl Pts',(20.8595802028306,20.6401872661395,3.75789612574311));
#138198=CARTESIAN_POINT('Ctrl Pts',(20.9041730844803,20.5689207574072,3.7620656916871));
#138199=CARTESIAN_POINT('Ctrl Pts',(20.9503337968388,20.4951486061425,3.76638185442608));
#138200=CARTESIAN_POINT('Ctrl Pts',(20.9927121598377,20.4190463693452,3.77069801716507));
#138201=CARTESIAN_POINT('Ctrl Pts',(21.0310846958975,20.3410450875402,3.77501417990405));
#138202=CARTESIAN_POINT('Ctrl Pts',(21.0682072506301,20.2655846892878,3.77918974409567));
#138203=CARTESIAN_POINT('Ctrl Pts',(21.1015808067414,20.1883475199542,3.7833653082873));
#138204=CARTESIAN_POINT('Ctrl Pts',(21.1310521424428,20.1097441384567,3.78754087247892));
#138205=CARTESIAN_POINT('Ctrl Pts',(21.1620120052503,20.0271706870183,3.79192733449158));
#138206=CARTESIAN_POINT('Ctrl Pts',(21.1886649090815,19.9430899381566,3.79631379650424));
#138207=CARTESIAN_POINT('Ctrl Pts',(21.2108930925539,19.8579935146962,3.80070025851691));
#138208=CARTESIAN_POINT('Ctrl Pts',(21.2331212760262,19.7728970912358,3.80508672052957));
#138209=CARTESIAN_POINT('Ctrl Pts',(21.2509246961548,19.6867855767775,3.80947318254223));
#138210=CARTESIAN_POINT('Ctrl Pts',(21.2642482087236,19.6001580684646,3.81385964455489));
#138211=CARTESIAN_POINT('Ctrl Pts',(21.2769586867287,19.5175164202231,3.818044278948));
#138212=CARTESIAN_POINT('Ctrl Pts',(21.285639763102,19.4340976099864,3.8222289133411));
#138213=CARTESIAN_POINT('Ctrl Pts',(21.2902056694013,19.3503290196652,3.82641354773421));
#138214=CARTESIAN_POINT('Ctrl Pts',(21.2947650766981,19.2666796635638,3.83059222581821));
#138215=CARTESIAN_POINT('Ctrl Pts',(21.2952209238071,19.1826819717238,3.83477090390222));
#138216=CARTESIAN_POINT('Ctrl Pts',(21.2915388082527,19.0987714640507,3.83894958198623));
#138217=CARTESIAN_POINT('Ctrl Pts',(21.2877906934233,19.0133569208346,3.84320315987165));
#138218=CARTESIAN_POINT('Ctrl Pts',(21.2797547375529,18.9280331946163,3.84745673775707));
#138219=CARTESIAN_POINT('Ctrl Pts',(21.2674501116906,18.843262958658,3.85171031564249));
#138220=CARTESIAN_POINT('Ctrl Pts',(21.2553840350109,18.7601361591377,3.8558814296205));
#138221=CARTESIAN_POINT('Ctrl Pts',(21.2392133934507,18.6775420566421,3.86005254359852));
#138222=CARTESIAN_POINT('Ctrl Pts',(21.2190086634415,18.5959130609251,3.86422365757653));
#138223=CARTESIAN_POINT('Ctrl Pts',(21.1988107133247,18.5143114566061,3.86839337189696));
#138224=CARTESIAN_POINT('Ctrl Pts',(21.1745814736228,18.433674762078,3.87256308621739));
#138225=CARTESIAN_POINT('Ctrl Pts',(21.1464423282957,18.3544242516582,3.87673280053782));
#138226=CARTESIAN_POINT('Ctrl Pts',(21.11830418428,18.2751765613115,3.88090236648192));
#138227=CARTESIAN_POINT('Ctrl Pts',(21.0862565659977,18.1973153902313,3.88507193242603));
#138228=CARTESIAN_POINT('Ctrl Pts',(21.0504699913875,18.1212446242384,3.88924149837013));
#138229=CARTESIAN_POINT('Ctrl Pts',(21.0134252049626,18.0424993039591,3.89355766110898));
#138230=CARTESIAN_POINT('Ctrl Pts',(20.9723738713789,17.9656731098162,3.89787382384784));
#138231=CARTESIAN_POINT('Ctrl Pts',(20.9275574633286,17.8911872651487,3.90218998658669));
#138232=CARTESIAN_POINT('Ctrl Pts',(20.8842009450553,17.8191277890345,3.90636555077843));
#138233=CARTESIAN_POINT('Ctrl Pts',(20.8373211816344,17.749258894982,3.91054111497017));
#138234=CARTESIAN_POINT('Ctrl Pts',(20.7871804520949,17.6819316460225,3.91471667916191));
#138235=CARTESIAN_POINT('Ctrl Pts',(20.734507233507,17.6112038577767,3.91910314117432));
#138236=CARTESIAN_POINT('Ctrl Pts',(20.6782353411158,17.5432816689316,3.92348960318672));
#138237=CARTESIAN_POINT('Ctrl Pts',(20.6187144099126,17.4785302042842,3.92787606519912));
#138238=CARTESIAN_POINT('Ctrl Pts',(20.5591934787095,17.4137787396368,3.93226252721153));
#138239=CARTESIAN_POINT('Ctrl Pts',(20.4964239761435,17.3521983512227,3.93664898922393));
#138240=CARTESIAN_POINT('Ctrl Pts',(20.4307957154099,17.2941055584183,3.94103545123633));
#138241=CARTESIAN_POINT('Ctrl Pts',(20.3864285506525,17.2548326524971,3.94400086401172));
#138242=CARTESIAN_POINT('Ctrl Pts',(20.3406387660481,17.2170491807618,3.94696627678711));
#138243=CARTESIAN_POINT('Ctrl Pts',(20.2935357313021,17.1808649545431,3.9499316895625));
#138244=CARTESIAN_POINT('Ctrl Pts',(20.2935357313021,17.1808649545431,3.14981136862994));
#138245=CARTESIAN_POINT('Ctrl Pts',(20.2269038112494,17.1296787734071,3.15398942161489));
#138246=CARTESIAN_POINT('Ctrl Pts',(20.1578180650956,17.081829284706,3.15816747459984));
#138247=CARTESIAN_POINT('Ctrl Pts',(20.0866541153584,17.0375403513743,3.16234552758478));
#138248=CARTESIAN_POINT('Ctrl Pts',(20.0153772777577,16.9931811622027,3.16653020824394));
#138249=CARTESIAN_POINT('Ctrl Pts',(19.9420160606565,16.9523940190638,3.1707148889031));
#138250=CARTESIAN_POINT('Ctrl Pts',(19.8669695044245,16.9153562771972,3.17489956956227));
#138251=CARTESIAN_POINT('Ctrl Pts',(19.8485514076067,16.9062663902008,3.17592658342408));
#138252=CARTESIAN_POINT('Ctrl Pts',(19.8300318839738,16.8974021064279,3.1769535972859));
#138253=CARTESIAN_POINT('Ctrl Pts',(19.8114169849418,16.8887655931067,3.17798061114772));
#138254=CARTESIAN_POINT('Ctrl Pts',(19.7355693750926,16.8535755610944,3.18216524554016));
#138255=CARTESIAN_POINT('Ctrl Pts',(19.6578547653245,16.8220398921686,3.1863498799326));
#138256=CARTESIAN_POINT('Ctrl Pts',(19.5786598305131,16.7943598176978,3.19053451432504));
#138257=CARTESIAN_POINT('Ctrl Pts',(19.499577619889,16.7667191423869,3.19471319240838));
#138258=CARTESIAN_POINT('Ctrl Pts',(19.4190197000616,16.7429233112,3.19889187049171));
#138259=CARTESIAN_POINT('Ctrl Pts',(19.3373948467029,16.7231264785017,3.20307054857505));
#138260=CARTESIAN_POINT('Ctrl Pts',(19.2543069264953,16.7029748018014,3.20732412646064));
#138261=CARTESIAN_POINT('Ctrl Pts',(19.1701138843274,16.6869671007256,3.21157770434622));
#138262=CARTESIAN_POINT('Ctrl Pts',(19.0852654759066,16.6752136199127,3.21583128223181));
#138263=CARTESIAN_POINT('Ctrl Pts',(19.0020620194663,16.6636880032626,3.22000239620915));
#138264=CARTESIAN_POINT('Ctrl Pts',(18.9182288577837,16.6562531921902,3.22417351018649));
#138265=CARTESIAN_POINT('Ctrl Pts',(18.8342009436324,16.6529617338876,3.22834462416382));
#138266=CARTESIAN_POINT('Ctrl Pts',(18.7502012258591,16.6496713800656,3.23251433848359));
#138267=CARTESIAN_POINT('Ctrl Pts',(18.6660073447032,16.6505216357631,3.23668405280335));
#138268=CARTESIAN_POINT('Ctrl Pts',(18.5820577129979,16.6555130519956,3.24085376712311));
#138269=CARTESIAN_POINT('Ctrl Pts',(18.4981110685808,16.6605042906122,3.24502333306654));
#138270=CARTESIAN_POINT('Ctrl Pts',(18.4144091155048,16.6696363686189,3.24919289900998));
#138271=CARTESIAN_POINT('Ctrl Pts',(18.3313872270485,16.6828578056098,3.25336246495342));
#138272=CARTESIAN_POINT('Ctrl Pts',(18.2454463913856,16.6965440920191,3.25767862769306));
#138273=CARTESIAN_POINT('Ctrl Pts',(18.1602348531237,16.7146125685865,3.26199479043271));
#138274=CARTESIAN_POINT('Ctrl Pts',(18.0762243702395,16.7369484199206,3.26631095317235));
#138275=CARTESIAN_POINT('Ctrl Pts',(17.9949505200243,16.7585566832401,3.27048651736343));
#138276=CARTESIAN_POINT('Ctrl Pts',(17.9148011124186,16.784158383043,3.27466208155451));
#138277=CARTESIAN_POINT('Ctrl Pts',(17.8361862981298,16.813599208156,3.27883764574559));
#138278=CARTESIAN_POINT('Ctrl Pts',(17.7536008364222,16.8445270193708,3.28322410775951));
#138279=CARTESIAN_POINT('Ctrl Pts',(17.6727096022458,16.8796917438774,3.28761056977344));
#138280=CARTESIAN_POINT('Ctrl Pts',(17.5939605452813,16.9188590702828,3.29199703178737));
#138281=CARTESIAN_POINT('Ctrl Pts',(17.5152114883168,16.9580263966883,3.2963834938013));
#138282=CARTESIAN_POINT('Ctrl Pts',(17.4386050767024,17.001195973874,3.30076995581523));
#138283=CARTESIAN_POINT('Ctrl Pts',(17.364553744478,17.0480813808105,3.30515641782915));
#138284=CARTESIAN_POINT('Ctrl Pts',(17.2939096238495,17.092809520654,3.30934105222176));
#138285=CARTESIAN_POINT('Ctrl Pts',(17.2253276726157,17.1410855493988,3.31352568661436));
#138286=CARTESIAN_POINT('Ctrl Pts',(17.1591863942882,17.19269325739,3.31771032100696));
#138287=CARTESIAN_POINT('Ctrl Pts',(17.0931392598839,17.2442275081965,3.32188899909045));
#138288=CARTESIAN_POINT('Ctrl Pts',(17.0295262575255,17.2990837381083,3.32606767717394));
#138289=CARTESIAN_POINT('Ctrl Pts',(16.9686982691563,17.3570016723092,3.33024635525743));
#138290=CARTESIAN_POINT('Ctrl Pts',(16.9067799828036,17.4159577438638,3.33449993314298));
#138291=CARTESIAN_POINT('Ctrl Pts',(16.8477479425957,17.4780861035064,3.33875351102853));
#138292=CARTESIAN_POINT('Ctrl Pts',(16.7919382910611,17.5430682511945,3.34300708891407));
#138293=CARTESIAN_POINT('Ctrl Pts',(16.7372106185328,17.6067905931384,3.34717820289155));
#138294=CARTESIAN_POINT('Ctrl Pts',(16.6855818186072,17.6732566930094,3.35134931686903));
#138295=CARTESIAN_POINT('Ctrl Pts',(16.6373315068437,17.742129267156,3.35552043084651));
#138296=CARTESIAN_POINT('Ctrl Pts',(16.5890973859384,17.810978730445,3.3596901451664));
#138297=CARTESIAN_POINT('Ctrl Pts',(16.5442397654171,17.8822326878121,3.36385985948629));
#138298=CARTESIAN_POINT('Ctrl Pts',(16.5029964131481,17.9555228016989,3.36802957380618));
#138299=CARTESIAN_POINT('Ctrl Pts',(16.4617545284947,18.0288103076089,3.37219913974973));
#138300=CARTESIAN_POINT('Ctrl Pts',(16.4241268812486,18.1041334246491,3.37636870569329));
#138301=CARTESIAN_POINT('Ctrl Pts',(16.3903058438335,18.1810982074242,3.38053827163684));
#138302=CARTESIAN_POINT('Ctrl Pts',(16.3552957004569,18.2607689770351,3.38485443437632));
#138303=CARTESIAN_POINT('Ctrl Pts',(16.3243650403573,18.3421985193633,3.3891705971158));
#138304=CARTESIAN_POINT('Ctrl Pts',(16.2976726756056,18.4249280132142,3.39348675985528));
#138305=CARTESIAN_POINT('Ctrl Pts',(16.2718498118346,18.5049626024846,3.39766232404646));
#138306=CARTESIAN_POINT('Ctrl Pts',(16.2499934356292,18.5862132848944,3.40183788823764));
#138307=CARTESIAN_POINT('Ctrl Pts',(16.2321958025117,18.6682516628952,3.40601345242882));
#138308=CARTESIAN_POINT('Ctrl Pts',(16.2134992532484,18.7544336043728,3.41039991444245));
#138309=CARTESIAN_POINT('Ctrl Pts',(16.1992823307861,18.8414843294194,3.41478637645608));
#138310=CARTESIAN_POINT('Ctrl Pts',(16.1895904829899,18.9289003549305,3.41917283846971));
#138311=CARTESIAN_POINT('Ctrl Pts',(16.1798986351937,19.0163163804415,3.42355930048334));
#138312=CARTESIAN_POINT('Ctrl Pts',(16.174731820223,19.1040971227329,3.42794576249697));
#138313=CARTESIAN_POINT('Ctrl Pts',(16.1740724460423,19.1917407557755,3.43233222451059));
#138314=CARTESIAN_POINT('Ctrl Pts',(16.1740244495167,19.1981204260764,3.43265151959756));
#138315=CARTESIAN_POINT('Ctrl Pts',(16.1740003013853,19.204500276023,3.43297081468453));
#138316=CARTESIAN_POINT('Ctrl Pts',(16.1740000028035,19.2108801913083,3.4332901097715));
#138317=CARTESIAN_POINT('',(16.174394460606,19.210617605254,3.3667098651142));
#138318=CARTESIAN_POINT('Ctrl Pts',(20.2933493626091,17.181116161832,3.08342410898733));
#138319=CARTESIAN_POINT('Ctrl Pts',(19.7793305315605,16.794397093965,3.11541446167017));
#138320=CARTESIAN_POINT('Ctrl Pts',(18.2370602654925,16.3326324953136,3.1897967499135));
#138321=CARTESIAN_POINT('Ctrl Pts',(16.4590845281242,17.5465283070756,3.28422525531049));
#138322=CARTESIAN_POINT('Ctrl Pts',(16.1776267405031,18.8060181972744,3.34666340802465));
#138323=CARTESIAN_POINT('Ctrl Pts',(16.1781627672566,19.2106133248248,3.36670962517832));
#138324=CARTESIAN_POINT('Ctrl Pts',(16.1740000284928,19.2106180532904,3.36670989022851));
#138325=CARTESIAN_POINT('Ctrl Pts',(16.1739869935966,19.297984518944,3.37103154303559));
#138326=CARTESIAN_POINT('Ctrl Pts',(16.1784506871913,19.3852864628672,3.37535319584266));
#138327=CARTESIAN_POINT('Ctrl Pts',(16.1873453738308,19.472055961455,3.37967484864974));
#138328=CARTESIAN_POINT('Ctrl Pts',(16.1966194662204,19.5625266412114,3.38418084296216));
#138329=CARTESIAN_POINT('Ctrl Pts',(16.2107109130556,19.6524179424094,3.38868683727458));
#138330=CARTESIAN_POINT('Ctrl Pts',(16.2295088315793,19.7412112666689,3.39319283158699));
#138331=CARTESIAN_POINT('Ctrl Pts',(16.2475982064586,19.8266577339084,3.39752898296558));
#138332=CARTESIAN_POINT('Ctrl Pts',(16.2700454505064,19.9110871351913,3.40186513434416));
#138333=CARTESIAN_POINT('Ctrl Pts',(16.2967009964589,19.9940540002691,3.40620128572275));
#138334=CARTESIAN_POINT('Ctrl Pts',(16.3233900671467,20.0771252129449,3.41054289068791));
#138335=CARTESIAN_POINT('Ctrl Pts',(16.354297844581,20.1587298407162,3.41488449565307));
#138336=CARTESIAN_POINT('Ctrl Pts',(16.3892268388774,20.2384428562597,3.41922610061823));
#138337=CARTESIAN_POINT('Ctrl Pts',(16.4242296046623,20.318324229007,3.42357687523362));
#138338=CARTESIAN_POINT('Ctrl Pts',(16.4632703651621,20.3963056454692,3.42792764984902));
#138339=CARTESIAN_POINT('Ctrl Pts',(16.5061059491326,20.4719869539808,3.43227842446442));
#138340=CARTESIAN_POINT('Ctrl Pts',(16.5109248522386,20.4805009243496,3.43276787644252));
#138341=CARTESIAN_POINT('Ctrl Pts',(16.5157917376009,20.4889858169829,3.43325732842063));
#138342=CARTESIAN_POINT('Ctrl Pts',(16.5207062260026,20.4974410868688,3.43374678039873));
#138343=CARTESIAN_POINT('Ctrl Pts',(16.5627232942887,20.5697305345463,3.43793141479118));
#138344=CARTESIAN_POINT('Ctrl Pts',(16.608363899273,20.6400938357955,3.44211604918362));
#138345=CARTESIAN_POINT('Ctrl Pts',(16.6574263400685,20.7081445604478,3.44630068357607));
#138346=CARTESIAN_POINT('Ctrl Pts',(16.706418946552,20.7760984233165,3.4504793616594));
#138347=CARTESIAN_POINT('Ctrl Pts',(16.7588234476461,20.8417458779044,3.45465803974274));
#138348=CARTESIAN_POINT('Ctrl Pts',(16.8143930615574,20.9047264247461,3.45883671782607));
#138349=CARTESIAN_POINT('Ctrl Pts',(16.8709587208711,20.9688358526381,3.46309029571166));
#138350=CARTESIAN_POINT('Ctrl Pts',(16.9308038360937,21.0301814068961,3.46734387359725));
#138351=CARTESIAN_POINT('Ctrl Pts',(16.9936228831501,21.0884151089051,3.47159745148283));
#138352=CARTESIAN_POINT('Ctrl Pts',(17.0552240603869,21.1455198369567,3.47576856546018));
#138353=CARTESIAN_POINT('Ctrl Pts',(17.1196845346185,21.1996319675306,3.47993967943753));
#138354=CARTESIAN_POINT('Ctrl Pts',(17.1866778681087,21.250459296029,3.48411079341487));
#138355=CARTESIAN_POINT('Ctrl Pts',(17.2536487213388,21.3012695689266,3.48828050773465));
#138356=CARTESIAN_POINT('Ctrl Pts',(17.3231503796756,21.3487969510059,3.49245022205442));
#138357=CARTESIAN_POINT('Ctrl Pts',(17.394823786903,21.3927898776635,3.49661993637419));
#138358=CARTESIAN_POINT('Ctrl Pts',(17.4664946436828,21.436781238864,3.50078950231762));
#138359=CARTESIAN_POINT('Ctrl Pts',(17.5403367031862,21.4772381547839,3.50495906826106));
#138360=CARTESIAN_POINT('Ctrl Pts',(17.6159635983351,21.513953452537,3.50912863420449));
#138361=CARTESIAN_POINT('Ctrl Pts',(17.694249441846,21.5519596148777,3.51344479694413));
#138362=CARTESIAN_POINT('Ctrl Pts',(17.7744474914061,21.5859559226942,3.51776095968377));
#138363=CARTESIAN_POINT('Ctrl Pts',(17.8561052781563,21.6157662791546,3.52207712242341));
#138364=CARTESIAN_POINT('Ctrl Pts',(17.9351030710676,21.6446055663798,3.5262526866145));
#138365=CARTESIAN_POINT('Ctrl Pts',(18.0154664958611,21.6695273345316,3.53042825080558));
#138366=CARTESIAN_POINT('Ctrl Pts',(18.0967709615464,21.6904231491521,3.53460381499666));
#138367=CARTESIAN_POINT('Ctrl Pts',(18.1821819225493,21.7123743617041,3.53899027701058));
#138368=CARTESIAN_POINT('Ctrl Pts',(18.2686309144573,21.7298821146794,3.5433767390245));
#138369=CARTESIAN_POINT('Ctrl Pts',(18.3556165397335,21.7428819002862,3.54776320103841));
#138370=CARTESIAN_POINT('Ctrl Pts',(18.4426021650096,21.755881685893,3.55214966305233));
#138371=CARTESIAN_POINT('Ctrl Pts',(18.5301238388031,21.7643735238079,3.55653612506624));
#138372=CARTESIAN_POINT('Ctrl Pts',(18.6176794289204,21.7683559636358,3.56092258708016));
#138373=CARTESIAN_POINT('Ctrl Pts',(18.7012064565128,21.7721551655022,3.56510722147276));
#138374=CARTESIAN_POINT('Ctrl Pts',(18.7850752514673,21.771864959913,3.56929185586537));
#138375=CARTESIAN_POINT('Ctrl Pts',(18.8688517103013,21.7674457780733,3.57347649025797));
#138376=CARTESIAN_POINT('Ctrl Pts',(18.9525089237153,21.7630328863919,3.57765516834146));
#138377=CARTESIAN_POINT('Ctrl Pts',(19.0360736066034,21.7545027162291,3.58183384642494));
#138378=CARTESIAN_POINT('Ctrl Pts',(19.119109057661,21.7418676404955,3.58601252450843));
#138379=CARTESIAN_POINT('Ctrl Pts',(19.2036328595138,21.7290060901084,3.59026610239398));
#138380=CARTESIAN_POINT('Ctrl Pts',(19.2876077883165,21.71189100391,3.59451968027953));
#138381=CARTESIAN_POINT('Ctrl Pts',(19.3705758747359,21.690590925073,3.59877325816508));
#138382=CARTESIAN_POINT('Ctrl Pts',(19.4519354628898,21.6697037898308,3.60294437214256));
#138383=CARTESIAN_POINT('Ctrl Pts',(19.5323264333863,21.6447926020538,3.60711548612004));
#138384=CARTESIAN_POINT('Ctrl Pts',(19.6113263938457,21.6159736794114,3.61128660009752));
#138385=CARTESIAN_POINT('Ctrl Pts',(19.6902998451052,21.587164427237,3.61545631441741));
#138386=CARTESIAN_POINT('Ctrl Pts',(19.7678827815191,21.5544502019412,3.6196260287373));
#138387=CARTESIAN_POINT('Ctrl Pts',(19.843669326747,21.5179967458314,3.62379574305719));
#138388=CARTESIAN_POINT('Ctrl Pts',(19.9194531751643,21.4815445868922,3.62796530900074));
#138389=CARTESIAN_POINT('Ctrl Pts',(19.9934403452927,21.4413536618681,3.63213487494429));
#138390=CARTESIAN_POINT('Ctrl Pts',(20.0652475043496,21.3976367055739,3.63630444088784));
#138391=CARTESIAN_POINT('Ctrl Pts',(20.1395793145537,21.3523827150158,3.64062060362732));
#138392=CARTESIAN_POINT('Ctrl Pts',(20.2115745125429,21.3033504035826,3.6449367663668));
#138393=CARTESIAN_POINT('Ctrl Pts',(20.2808401159379,21.2508249081049,3.64925292910628));
#138394=CARTESIAN_POINT('Ctrl Pts',(20.3478493995712,21.2000104251303,3.65342849329747));
#138395=CARTESIAN_POINT('Ctrl Pts',(20.412303860261,21.1459271830854,3.65760405748865));
#138396=CARTESIAN_POINT('Ctrl Pts',(20.4738824987383,21.088873502285,3.66177962167984));
#138397=CARTESIAN_POINT('Ctrl Pts',(20.5385713278795,21.0289381756777,3.66616608369346));
#138398=CARTESIAN_POINT('Ctrl Pts',(20.6000857771511,20.9657248689593,3.67055254570709));
#138399=CARTESIAN_POINT('Ctrl Pts',(20.6581002087315,20.8996202612664,3.67493900772071));
#138400=CARTESIAN_POINT('Ctrl Pts',(20.716114640312,20.8335156535734,3.67932546973434));
#138401=CARTESIAN_POINT('Ctrl Pts',(20.7706287541777,20.7645202473234,3.68371193174797));
#138402=CARTESIAN_POINT('Ctrl Pts',(20.8213695361432,20.6930554711554,3.6880983937616));
#138403=CARTESIAN_POINT('Ctrl Pts',(20.8697756595073,20.6248788952852,3.69228302815506));
#138404=CARTESIAN_POINT('Ctrl Pts',(20.914928230553,20.5542014284548,3.69646766254852));
#138405=CARTESIAN_POINT('Ctrl Pts',(20.956559006204,20.4813666651568,3.70065229694198));
#138406=CARTESIAN_POINT('Ctrl Pts',(20.9981305255987,20.4086355731291,3.70483097502634));
#138407=CARTESIAN_POINT('Ctrl Pts',(21.0361899803433,20.3337536798786,3.70900965311069));
#138408=CARTESIAN_POINT('Ctrl Pts',(21.0705113959643,20.2570948793149,3.71318833119505));
#138409=CARTESIAN_POINT('Ctrl Pts',(21.1054479982897,20.1790620248545,3.71744190908039));
#138410=CARTESIAN_POINT('Ctrl Pts',(21.1365109555626,20.099188327509,3.72169548696572));
#138411=CARTESIAN_POINT('Ctrl Pts',(21.1635100116305,20.0178959681318,3.72594906485105));
#138412=CARTESIAN_POINT('Ctrl Pts',(21.1899856383155,19.9381796197599,3.73012017882943));
#138413=CARTESIAN_POINT('Ctrl Pts',(21.2125533792703,19.857099582236,3.73429129280781));
#138414=CARTESIAN_POINT('Ctrl Pts',(21.2310824062636,19.7750739812547,3.73846240678619));
#138415=CARTESIAN_POINT('Ctrl Pts',(21.2496052156631,19.693075904756,3.742632121107));
#138416=CARTESIAN_POINT('Ctrl Pts',(21.2640919013284,19.6101333433019,3.74680183542781));
#138417=CARTESIAN_POINT('Ctrl Pts',(21.2744621331458,19.526677287831,3.75097154974862));
#138418=CARTESIAN_POINT('Ctrl Pts',(21.2848319959459,19.4432242020848,3.7551411156931));
#138419=CARTESIAN_POINT('Ctrl Pts',(21.2910856402585,19.3592581152789,3.75931068163757));
#138420=CARTESIAN_POINT('Ctrl Pts',(21.293194451632,19.2752164989405,3.76348024758204));
#138421=CARTESIAN_POINT('Ctrl Pts',(21.2953774062114,19.1882200830673,3.76779641032046));
#138422=CARTESIAN_POINT('Ctrl Pts',(21.2931186269949,19.1011432548623,3.77211257305888));
#138423=CARTESIAN_POINT('Ctrl Pts',(21.2864451550249,19.0144707894736,3.77642873579729));
#138424=CARTESIAN_POINT('Ctrl Pts',(21.2799890707009,18.93062167051,3.78060429998941));
#138425=CARTESIAN_POINT('Ctrl Pts',(21.2694016000863,18.847151436045,3.78477986418152));
#138426=CARTESIAN_POINT('Ctrl Pts',(21.2547598325397,18.7644914707931,3.78895542837364));
#138427=CARTESIAN_POINT('Ctrl Pts',(21.2393785441268,18.67765654723,3.7933418903852));
#138428=CARTESIAN_POINT('Ctrl Pts',(21.2195227615801,18.591716466318,3.79772835239677));
#138429=CARTESIAN_POINT('Ctrl Pts',(21.1953413592831,18.5071543400132,3.80211481440834));
#138430=CARTESIAN_POINT('Ctrl Pts',(21.1711599569862,18.4225922137084,3.8065012764199));
#138431=CARTESIAN_POINT('Ctrl Pts',(21.1426531949957,18.3394085662325,3.81088773843147));
#138432=CARTESIAN_POINT('Ctrl Pts',(21.1100276507034,18.2580610706384,3.81527420044303));
#138433=CARTESIAN_POINT('Ctrl Pts',(21.0789046619562,18.1804599993028,3.81945864581514));
#138434=CARTESIAN_POINT('Ctrl Pts',(21.0439180829639,18.1042408407741,3.82364309118724));
#138435=CARTESIAN_POINT('Ctrl Pts',(21.0052116068273,18.0298150707814,3.82782753655935));
#138436=CARTESIAN_POINT('Ctrl Pts',(20.9665579257085,17.9554908163553,3.83200627441451));
#138437=CARTESIAN_POINT('Ctrl Pts',(20.9241946333113,17.8829554976095,3.83618501226968));
#138438=CARTESIAN_POINT('Ctrl Pts',(20.8783138059651,17.8126015226168,3.84036375012484));
#138439=CARTESIAN_POINT('Ctrl Pts',(20.8324875829291,17.7423312782476,3.84453751472404));
#138440=CARTESIAN_POINT('Ctrl Pts',(20.7831523972201,17.6742375999625,3.84871127932324));
#138441=CARTESIAN_POINT('Ctrl Pts',(20.7305459075039,17.6086877834737,3.85288504392244));
#138442=CARTESIAN_POINT('Ctrl Pts',(20.6779756656234,17.543183133256,3.85705593264199));
#138443=CARTESIAN_POINT('Ctrl Pts',(20.6221388841159,17.4802192208246,3.86122682136153));
#138444=CARTESIAN_POINT('Ctrl Pts',(20.5633154981094,17.4201329450859,3.86539771008108));
#138445=CARTESIAN_POINT('Ctrl Pts',(20.5045103316182,17.3600652800204,3.86956730694078));
#138446=CARTESIAN_POINT('Ctrl Pts',(20.4427207177847,17.302873811311,3.87373690380047));
#138447=CARTESIAN_POINT('Ctrl Pts',(20.3782648488343,17.2488600694935,3.87790650066017));
#138448=CARTESIAN_POINT('Ctrl Pts',(20.3505067138017,17.2255988713528,3.87970215146044));
#138449=CARTESIAN_POINT('Ctrl Pts',(20.3222545464684,17.2029265501561,3.88149780226072));
#138450=CARTESIAN_POINT('Ctrl Pts',(20.2935357313021,17.1808649545432,3.88329345306099));
#138451=CARTESIAN_POINT('Origin',(18.734,19.211,-1.76670989022852));
#138452=CARTESIAN_POINT('',(20.2917777939293,17.1831894823609,4.74997346808548));
#138453=CARTESIAN_POINT('',(20.2944552424268,17.1796893591268,4.68319930761182));
#138454=CARTESIAN_POINT('',(20.2935357313021,17.1808649545432,-1.76670989022852));
#138455=CARTESIAN_POINT('',(16.1740009581142,19.2087851537238,4.23329008724976));
#138456=CARTESIAN_POINT('Ctrl Pts',(16.1756127741342,19.2087870016449,4.2332901097715));
#138457=CARTESIAN_POINT('Ctrl Pts',(16.1805387735992,19.8078855990186,4.26304769694121));
#138458=CARTESIAN_POINT('Ctrl Pts',(16.6895187210545,21.2679843244803,4.3351972196714));
#138459=CARTESIAN_POINT('Ctrl Pts',(19.1239734425187,22.2128679703362,4.44973867796207));
#138460=CARTESIAN_POINT('Ctrl Pts',(21.469181135151,20.5079482468907,4.5769144846435));
#138461=CARTESIAN_POINT('Ctrl Pts',(21.340005854912,18.2299561683482,4.67699274801797));
#138462=CARTESIAN_POINT('Ctrl Pts',(20.5375803645769,17.3693101922807,4.73467907583197));
#138463=CARTESIAN_POINT('Ctrl Pts',(20.2917777939292,17.1831894823608,4.74997346808549));
#138464=CARTESIAN_POINT('Ctrl Pts',(20.2935357313021,17.1808649545431,3.9499316895625));
#138465=CARTESIAN_POINT('Ctrl Pts',(20.2271357280555,17.129856930297,3.95411195987788));
#138466=CARTESIAN_POINT('Ctrl Pts',(20.1581247140608,17.082028628014,3.95829223019326));
#138467=CARTESIAN_POINT('Ctrl Pts',(20.086840669308,17.0376564644616,3.96247250050864));
#138468=CARTESIAN_POINT('Ctrl Pts',(20.0156413539939,16.9933370424243,3.966647802083));
#138469=CARTESIAN_POINT('Ctrl Pts',(19.9421747637508,16.952465839246,3.97082310365735));
#138470=CARTESIAN_POINT('Ctrl Pts',(19.8668100020607,16.9152775648543,3.9749984052317));
#138471=CARTESIAN_POINT('Ctrl Pts',(19.7915083801787,16.8781204464094,3.97917020878212));
#138472=CARTESIAN_POINT('Ctrl Pts',(19.7143121580704,16.8446403283179,3.98334201233255));
#138473=CARTESIAN_POINT('Ctrl Pts',(19.6356161995566,16.8150266636089,3.98751381588297));
#138474=CARTESIAN_POINT('Ctrl Pts',(19.5569539799023,16.7854256949937,3.99168383088037));
#138475=CARTESIAN_POINT('Ctrl Pts',(19.4767937305971,16.7596880499491,3.99585384587777));
#138476=CARTESIAN_POINT('Ctrl Pts',(19.3955503834759,16.7379550974309,4.00002386087518));
#138477=CARTESIAN_POINT('Ctrl Pts',(19.3143174962085,16.7162249429696,4.00419333899481));
#138478=CARTESIAN_POINT('Ctrl Pts',(19.2320022326464,16.6984985750593,4.00836281711444));
#138479=CARTESIAN_POINT('Ctrl Pts',(19.1490334553667,16.6848671390985,4.01253229523407));
#138480=CARTESIAN_POINT('Ctrl Pts',(19.0660504717973,16.6712333691015,4.01670248727063));
#138481=CARTESIAN_POINT('Ctrl Pts',(18.982414206433,16.6616959965769,4.02087267930718));
#138482=CARTESIAN_POINT('Ctrl Pts',(18.8985610919208,16.6562946066081,4.02504287134374));
#138483=CARTESIAN_POINT('Ctrl Pts',(18.8146155488082,16.6508872628602,4.0292176600493));
#138484=CARTESIAN_POINT('Ctrl Pts',(18.7304531392929,16.6496250299137,4.03339244875486));
#138485=CARTESIAN_POINT('Ctrl Pts',(18.6465122154691,16.652495380587,4.03756723746043));
#138486=CARTESIAN_POINT('Ctrl Pts',(18.5625187191745,16.6553675289701,4.0417446408496));
#138487=CARTESIAN_POINT('Ctrl Pts',(18.4787474427678,16.6623773741964,4.04592204423879));
#138488=CARTESIAN_POINT('Ctrl Pts',(18.3956311376542,16.6734605396182,4.05009944762796));
#138489=CARTESIAN_POINT('Ctrl Pts',(18.3123782640378,16.6845619158027,4.05428371491377));
#138490=CARTESIAN_POINT('Ctrl Pts',(18.2297829614727,16.6997498876352,4.05846798219958));
#138491=CARTESIAN_POINT('Ctrl Pts',(18.148266884597,16.718909167482,4.06265224948539));
#138492=CARTESIAN_POINT('Ctrl Pts',(18.1121674891097,16.7273938547603,4.06450525229618));
#138493=CARTESIAN_POINT('Ctrl Pts',(18.0762795331303,16.7366567267922,4.06635825510697));
#138494=CARTESIAN_POINT('Ctrl Pts',(18.040638468227,16.7466847226344,4.06821125791776));
#138495=CARTESIAN_POINT('Ctrl Pts',(17.960150287027,16.7693309356085,4.07239589231081));
#138496=CARTESIAN_POINT('Ctrl Pts',(17.8806229756134,16.7959667334644,4.07658052670385));
#138497=CARTESIAN_POINT('Ctrl Pts',(17.8024810747699,16.8264932392761,4.08076516109689));
#138498=CARTESIAN_POINT('Ctrl Pts',(17.7244503992502,16.8569762943851,4.08494383918083));
#138499=CARTESIAN_POINT('Ctrl Pts',(17.6478016421982,16.8913388913935,4.08912251726477));
#138500=CARTESIAN_POINT('Ctrl Pts',(17.5729454850808,16.9294320274457,4.0933011953487));
#138501=CARTESIAN_POINT('Ctrl Pts',(17.496747585145,16.9682079555846,4.09755477323414));
#138502=CARTESIAN_POINT('Ctrl Pts',(17.4224076460745,17.0108493474659,4.10180835111958));
#138503=CARTESIAN_POINT('Ctrl Pts',(17.3503388850128,17.0571471919204,4.10606192900502));
#138504=CARTESIAN_POINT('Ctrl Pts',(17.279667317515,17.1025474623173,4.11023304298296));
#138505=CARTESIAN_POINT('Ctrl Pts',(17.2111800563177,17.1514634154306,4.1144041569609));
#138506=CARTESIAN_POINT('Ctrl Pts',(17.1452415288499,17.2036518686713,4.11857527093885));
#138507=CARTESIAN_POINT('Ctrl Pts',(17.0793251276917,17.2558228095726,4.12274498525921));
#138508=CARTESIAN_POINT('Ctrl Pts',(17.0159561221395,17.3112637844565,4.12691469957958));
#138509=CARTESIAN_POINT('Ctrl Pts',(16.9554677262144,17.3696898818767,4.13108441389994));
#138510=CARTESIAN_POINT('Ctrl Pts',(16.8949814827259,17.4281139002458,4.13525397984399));
#138511=CARTESIAN_POINT('Ctrl Pts',(16.8373759753513,17.4895225097358,4.13942354578803));
#138512=CARTESIAN_POINT('Ctrl Pts',(16.7829482470742,17.5535932733921,4.14359311173208));
#138513=CARTESIAN_POINT('Ctrl Pts',(16.7266069070147,17.6199166860587,4.14790927447101));
#138514=CARTESIAN_POINT('Ctrl Pts',(16.6736713066578,17.6890925366905,4.15222543720993));
#138515=CARTESIAN_POINT('Ctrl Pts',(16.6244248933202,17.7607266225718,4.15654159994886));
#138516=CARTESIAN_POINT('Ctrl Pts',(16.5767826767175,17.8300272356399,4.16071716414053));
#138517=CARTESIAN_POINT('Ctrl Pts',(16.5325931948251,17.9016279637396,4.16489272833221));
#138518=CARTESIAN_POINT('Ctrl Pts',(16.4920674161604,17.9751447133591,4.16906829252389));
#138519=CARTESIAN_POINT('Ctrl Pts',(16.449494776756,18.0523746192327,4.17345475453644));
#138520=CARTESIAN_POINT('Ctrl Pts',(16.4109659295263,18.1317186646457,4.17784121654899));
#138521=CARTESIAN_POINT('Ctrl Pts',(16.3766684749371,18.2127074171643,4.18222767856154));
#138522=CARTESIAN_POINT('Ctrl Pts',(16.342371020348,18.293696169683,4.18661414057409));
#138523=CARTESIAN_POINT('Ctrl Pts',(16.3123050853067,18.3763290580522,4.19100060258664));
#138524=CARTESIAN_POINT('Ctrl Pts',(16.2865973915759,18.4601202011779,4.1953870645992));
#138525=CARTESIAN_POINT('Ctrl Pts',(16.256634152739,18.557781782967,4.20049964335899));
#138526=CARTESIAN_POINT('Ctrl Pts',(16.2324986213398,18.6573099274652,4.20561222211878));
#138527=CARTESIAN_POINT('Ctrl Pts',(16.2143850329176,18.7580757042789,4.21072480087858));
#138528=CARTESIAN_POINT('Ctrl Pts',(16.1965183144929,18.8574681448718,4.21576770033044));
#138529=CARTESIAN_POINT('Ctrl Pts',(16.184510545625,18.9580647258724,4.2208105997823));
#138530=CARTESIAN_POINT('Ctrl Pts',(16.1785021632639,19.0592409592912,4.22585349923416));
#138531=CARTESIAN_POINT('Ctrl Pts',(16.1755487125961,19.1089746473601,4.22833236190603));
#138532=CARTESIAN_POINT('Ctrl Pts',(16.1740441624119,19.1588480714529,4.23081122457789));
#138533=CARTESIAN_POINT('Ctrl Pts',(16.1740009581142,19.2087851537238,4.23329008724976));
#138534=CARTESIAN_POINT('',(16.1740010840393,19.2133559031925,4.16670989022851));
#138535=CARTESIAN_POINT('Ctrl Pts',(20.2935357313021,17.1808649545432,3.88329345306099));
#138536=CARTESIAN_POINT('Ctrl Pts',(20.2268447748805,17.1296334220759,3.88746332109265));
#138537=CARTESIAN_POINT('Ctrl Pts',(20.1576354377003,17.0816982854579,3.89163318912431));
#138538=CARTESIAN_POINT('Ctrl Pts',(20.0862723391846,17.0373027992206,3.89580305715597));
#138539=CARTESIAN_POINT('Ctrl Pts',(20.0148340436107,16.9928605323637,3.8999773190805));
#138540=CARTESIAN_POINT('Ctrl Pts',(19.9412378466428,16.9519656067142,3.90415158100503));
#138541=CARTESIAN_POINT('Ctrl Pts',(19.8658750615154,16.9148164609249,3.90832584292955));
#138542=CARTESIAN_POINT('Ctrl Pts',(19.7904707123725,16.8776468266721,3.91250240703927));
#138543=CARTESIAN_POINT('Ctrl Pts',(19.7132982573728,16.844227268621,3.91667897114898));
#138544=CARTESIAN_POINT('Ctrl Pts',(19.6347689490016,16.8147080101719,3.92085553525869));
#138545=CARTESIAN_POINT('Ctrl Pts',(19.5561040137784,16.7851377694311,3.9250393126529));
#138546=CARTESIAN_POINT('Ctrl Pts',(19.4760779832782,16.7594814223516,3.92922309004711));
#138547=CARTESIAN_POINT('Ctrl Pts',(19.3951169799099,16.7378392007646,3.93340686744132));
#138548=CARTESIAN_POINT('Ctrl Pts',(19.3367851907664,16.7222461441856,3.9364212473357));
#138549=CARTESIAN_POINT('Ctrl Pts',(19.2779683349948,16.708735793246,3.93943562723009));
#138550=CARTESIAN_POINT('Ctrl Pts',(19.2188278686569,16.6973289917387,3.94245000712447));
#138551=CARTESIAN_POINT('Ctrl Pts',(19.1367276562993,16.6814937965827,3.94663464151747));
#138552=CARTESIAN_POINT('Ctrl Pts',(19.0536980417284,16.6696556340513,3.95081927591047));
#138553=CARTESIAN_POINT('Ctrl Pts',(18.9701628470245,16.6619164176737,3.95500391030348));
#138554=CARTESIAN_POINT('Ctrl Pts',(18.8867465543309,16.6541882171128,3.95918258838736));
#138555=CARTESIAN_POINT('Ctrl Pts',(18.8028265650706,16.6505474159413,3.96336126647125));
#138556=CARTESIAN_POINT('Ctrl Pts',(18.7188367813175,16.651044907269,3.96753994455514));
#138557=CARTESIAN_POINT('Ctrl Pts',(18.6333415410517,16.6515513157713,3.97179352244059));
#138558=CARTESIAN_POINT('Ctrl Pts',(18.5477744529634,16.6563459251098,3.97604710032604));
#138559=CARTESIAN_POINT('Ctrl Pts',(18.4625985845179,16.6654271230872,3.98030067821149));
#138560=CARTESIAN_POINT('Ctrl Pts',(18.3790740164904,16.6743322643211,3.98447179218939));
#138561=CARTESIAN_POINT('Ctrl Pts',(18.2959261128669,16.6873592186152,3.98864290616729));
#138562=CARTESIAN_POINT('Ctrl Pts',(18.2135896449265,16.7044539576676,3.9928140201452));
#138563=CARTESIAN_POINT('Ctrl Pts',(18.1312808057832,16.7215429604151,3.99698373446551));
#138564=CARTESIAN_POINT('Ctrl Pts',(18.049783311613,16.7426969435999,4.00115344878583));
#138565=CARTESIAN_POINT('Ctrl Pts',(17.9695227367355,16.7678105857401,4.00532316310615));
#138566=CARTESIAN_POINT('Ctrl Pts',(17.8892650178734,16.7929233342292,4.00949272905015));
#138567=CARTESIAN_POINT('Ctrl Pts',(17.8102445695787,16.8219953233349,4.01366229499415));
#138568=CARTESIAN_POINT('Ctrl Pts',(17.7328714533942,16.8548714735458,4.01783186093816));
#138569=CARTESIAN_POINT('Ctrl Pts',(17.652777993893,16.8889035086419,4.02214802367714));
#138570=CARTESIAN_POINT('Ctrl Pts',(17.5744503476379,16.9270119844461,4.02646418641611));
#138571=CARTESIAN_POINT('Ctrl Pts',(17.4983185918994,16.9689715751859,4.03078034915509));
#138572=CARTESIAN_POINT('Ctrl Pts',(17.4246668200984,17.0095643366696,4.03495591334672));
#138573=CARTESIAN_POINT('Ctrl Pts',(17.3530704495475,17.0537608783684,4.03913147753835));
#138574=CARTESIAN_POINT('Ctrl Pts',(17.2838902366718,17.1013124225847,4.04330704172998));
#138575=CARTESIAN_POINT('Ctrl Pts',(17.2112158957015,17.1512656822582,4.04769350374263));
#138576=CARTESIAN_POINT('Ctrl Pts',(17.141208670627,17.2049214186627,4.05207996575528));
#138577=CARTESIAN_POINT('Ctrl Pts',(17.0742466821562,17.261944094207,4.05646642776793));
#138578=CARTESIAN_POINT('Ctrl Pts',(17.0072846936854,17.3189667697514,4.06085288978059));
#138579=CARTESIAN_POINT('Ctrl Pts',(16.9433683113269,17.3793559306723,4.06523935179324));
#138580=CARTESIAN_POINT('Ctrl Pts',(16.8828286089282,17.4427340469043,4.06962581380589));
#138581=CARTESIAN_POINT('Ctrl Pts',(16.8258191500137,17.5024164036099,4.07375648865202));
#138582=CARTESIAN_POINT('Ctrl Pts',(16.7715797255597,17.5649836670307,4.07788716349815));
#138583=CARTESIAN_POINT('Ctrl Pts',(16.720421868205,17.6301448177784,4.08201783834428));
#138584=CARTESIAN_POINT('Ctrl Pts',(16.6693300782615,17.6952218166721,4.08614317866297));
#138585=CARTESIAN_POINT('Ctrl Pts',(16.6213122506322,17.7628856907896,4.09026851898165));
#138586=CARTESIAN_POINT('Ctrl Pts',(16.5766430483354,17.8328088002369,4.09439385930034));
#138587=CARTESIAN_POINT('Ctrl Pts',(16.5320173182039,17.9026638603613,4.09851518482882));
#138588=CARTESIAN_POINT('Ctrl Pts',(16.4907340001792,17.9747733973529,4.10263651035731));
#138589=CARTESIAN_POINT('Ctrl Pts',(16.4530264539488,18.0487781269419,4.10675783588579));
#138590=CARTESIAN_POINT('Ctrl Pts',(16.4153436115609,18.1227343728356,4.11087646135587));
#138591=CARTESIAN_POINT('Ctrl Pts',(16.3812321043788,18.1985829265154,4.11499508682596));
#138592=CARTESIAN_POINT('Ctrl Pts',(16.350880245421,18.2759383788566,4.11911371229604));
#138593=CARTESIAN_POINT('Ctrl Pts',(16.3205285952524,18.3532932990729,4.12323230943428));
#138594=CARTESIAN_POINT('Ctrl Pts',(16.293936732308,18.4321546644583,4.12735090657251));
#138595=CARTESIAN_POINT('Ctrl Pts',(16.271245067881,18.5121165016089,4.13146950371074));
#138596=CARTESIAN_POINT('Ctrl Pts',(16.2485547151171,18.592073716666,4.13558786277865));
#138597=CARTESIAN_POINT('Ctrl Pts',(16.2297642345969,18.6731308198829,4.13970622184656));
#138598=CARTESIAN_POINT('Ctrl Pts',(16.2149637529306,18.7548680169618,4.14382458091447));
#138599=CARTESIAN_POINT('Ctrl Pts',(16.2001500672814,18.8366781344071,4.14794661410215));
#138600=CARTESIAN_POINT('Ctrl Pts',(16.1893335672673,18.9191690901925,4.15206864728983));
#138601=CARTESIAN_POINT('Ctrl Pts',(16.1825528364003,19.0019130052847,4.15619068047751));
#138602=CARTESIAN_POINT('Ctrl Pts',(16.1767848147302,19.0722990307275,4.15969708372784));
#138603=CARTESIAN_POINT('Ctrl Pts',(16.1739362156169,19.1428678239494,4.16320348697818));
#138604=CARTESIAN_POINT('Ctrl Pts',(16.1740010840393,19.2133559031925,4.16670989022851));
#138605=CARTESIAN_POINT('Ctrl Pts',(16.1740881651155,19.2133565881468,4.16670992828903));
#138606=CARTESIAN_POINT('Ctrl Pts',(16.1722334682522,19.4149927583358,4.17674049235513));
#138607=CARTESIAN_POINT('Ctrl Pts',(16.2862272813843,20.4667260563269,4.22916299198171));
#138608=CARTESIAN_POINT('Ctrl Pts',(17.7370129313198,22.0692002669558,4.32397742716876));
#138609=CARTESIAN_POINT('Ctrl Pts',(20.5976439135897,21.5963979425813,4.4511532338502));
#138610=CARTESIAN_POINT('Ctrl Pts',(21.6812140247095,19.0907282283214,4.57089386066455));
#138611=CARTESIAN_POINT('Ctrl Pts',(20.8466207950879,17.6125715727613,4.64824255191842));
#138612=CARTESIAN_POINT('Ctrl Pts',(20.2944552424269,17.1796893591269,4.68319930761182));
#138613=CARTESIAN_POINT('Origin',(18.734,19.211,-1.76670989022852));
#138614=CARTESIAN_POINT('',(20.2935357313021,17.1808649545431,5.54983331802439));
#138615=CARTESIAN_POINT('',(20.2935357313021,17.1808649545431,5.48336965260678));
#138616=CARTESIAN_POINT('',(20.2935357313021,17.1808649545432,-1.76670989022852));
#138617=CARTESIAN_POINT('',(16.1741505041835,19.2121967451321,5.03329016024809));
#138618=CARTESIAN_POINT('Ctrl Pts',(16.1740002797795,19.2121968587701,5.03329016239966));
#138619=CARTESIAN_POINT('Ctrl Pts',(16.1740435234787,19.3046921980315,5.03786858507908));
#138620=CARTESIAN_POINT('Ctrl Pts',(16.1791038614083,19.3970207371689,5.0424470077585));
#138621=CARTESIAN_POINT('Ctrl Pts',(16.1891023385012,19.4886614710357,5.04702543043792));
#138622=CARTESIAN_POINT('Ctrl Pts',(16.199131888135,19.5805869993194,5.05161808160682));
#138623=CARTESIAN_POINT('Ctrl Pts',(16.2141301908471,19.6718201549905,5.05621073277571));
#138624=CARTESIAN_POINT('Ctrl Pts',(16.2339673694789,19.7618510200861,5.0608033839446));
#138625=CARTESIAN_POINT('Ctrl Pts',(16.2538962421947,19.8522980379953,5.06541726388547));
#138626=CARTESIAN_POINT('Ctrl Pts',(16.2787086950664,19.9415313458139,5.07003114382633));
#138627=CARTESIAN_POINT('Ctrl Pts',(16.3082244096461,20.0290542679085,5.07464502376719));
#138628=CARTESIAN_POINT('Ctrl Pts',(16.331622411587,20.0984363421765,5.07830258630121));
#138629=CARTESIAN_POINT('Ctrl Pts',(16.3579750606107,20.1667439285256,5.08196014883522));
#138630=CARTESIAN_POINT('Ctrl Pts',(16.3871718743355,20.233740313369,5.08561771136923));
#138631=CARTESIAN_POINT('Ctrl Pts',(16.4205760854035,20.310391190454,5.08980234576228));
#138632=CARTESIAN_POINT('Ctrl Pts',(16.457801705802,20.385546444256,5.09398698015532));
#138633=CARTESIAN_POINT('Ctrl Pts',(16.4986929228154,20.4587989704629,5.09817161454837));
#138634=CARTESIAN_POINT('Ctrl Pts',(16.5395259362427,20.5319472307656,5.10235029263232));
#138635=CARTESIAN_POINT('Ctrl Pts',(16.5840139603303,20.6031977447539,5.10652897071627));
#138636=CARTESIAN_POINT('Ctrl Pts',(16.6319534129312,20.6721639695094,5.11070764880021));
#138637=CARTESIAN_POINT('Ctrl Pts',(16.6807521457666,20.7423663642785,5.11496122668565));
#138638=CARTESIAN_POINT('Ctrl Pts',(16.7331270652481,20.8102013305708,5.11921480457108));
#138639=CARTESIAN_POINT('Ctrl Pts',(16.7888147952353,20.8752879916542,5.12346838245652));
#138640=CARTESIAN_POINT('Ctrl Pts',(16.843422909911,20.9391128208063,5.12763949643447));
#138641=CARTESIAN_POINT('Ctrl Pts',(16.9012162179244,21.0002945906744,5.13181061041243));
#138642=CARTESIAN_POINT('Ctrl Pts',(16.9619041398262,21.0585054160556,5.13598172439038));
#138643=CARTESIAN_POINT('Ctrl Pts',(17.0225716973097,21.1166967082321,5.14015143871075));
#138644=CARTESIAN_POINT('Ctrl Pts',(17.0861316079122,21.1719187176575,5.14432115303112));
#138645=CARTESIAN_POINT('Ctrl Pts',(17.1522562065727,21.2238801683047,5.14849086735149));
#138646=CARTESIAN_POINT('Ctrl Pts',(17.2183784522363,21.2758397699405,5.15266043329554));
#138647=CARTESIAN_POINT('Ctrl Pts',(17.2870648422624,21.3245387599152,5.15682999923959));
#138648=CARTESIAN_POINT('Ctrl Pts',(17.3579554657572,21.3697268098999,5.16099956518364));
#138649=CARTESIAN_POINT('Ctrl Pts',(17.431338516121,21.4165036159765,5.16531572792255));
#138650=CARTESIAN_POINT('Ctrl Pts',(17.5070832408527,21.459517715654,5.16963189066148));
#138651=CARTESIAN_POINT('Ctrl Pts',(17.5847604857697,21.4985420299815,5.17394805340039));
#138652=CARTESIAN_POINT('Ctrl Pts',(17.6599074026038,21.5362951313743,5.17812361759207));
#138653=CARTESIAN_POINT('Ctrl Pts',(17.736862419498,21.5703142429023,5.18229918178375));
#138654=CARTESIAN_POINT('Ctrl Pts',(17.8152162748904,21.6004427104398,5.18647474597543));
#138655=CARTESIAN_POINT('Ctrl Pts',(17.8975275972501,21.6320928952489,5.19086120798797));
#138656=CARTESIAN_POINT('Ctrl Pts',(17.9813822273946,21.6594488930309,5.19524767000051));
#138657=CARTESIAN_POINT('Ctrl Pts',(18.0662895457781,21.6823888300554,5.19963413201305));
#138658=CARTESIAN_POINT('Ctrl Pts',(18.1511968641616,21.70532876708,5.20402059402559));
#138659=CARTESIAN_POINT('Ctrl Pts',(18.2371562875637,21.723852595477,5.20840705603813));
#138660=CARTESIAN_POINT('Ctrl Pts',(18.3236691980734,21.7379009939035,5.21279351805067));
#138661=CARTESIAN_POINT('Ctrl Pts',(18.4062015213278,21.7513030046936,5.21697815244372));
#138662=CARTESIAN_POINT('Ctrl Pts',(18.4895447184805,21.7606822624715,5.22116278683676));
#138663=CARTESIAN_POINT('Ctrl Pts',(18.5732721407629,21.7659494232303,5.22534742122981));
#138664=CARTESIAN_POINT('Ctrl Pts',(18.6568803874232,21.7712090868378,5.22952609931376));
#138665=CARTESIAN_POINT('Ctrl Pts',(18.7408713177055,21.7723682508116,5.2337047773977));
#138666=CARTESIAN_POINT('Ctrl Pts',(18.8248097150324,21.7693888671693,5.23788345548165));
#138667=CARTESIAN_POINT('Ctrl Pts',(18.910252647806,21.7663560802164,5.24213703336708));
#138668=CARTESIAN_POINT('Ctrl Pts',(18.9956406698881,21.7590348421053,5.24639061125252));
#138669=CARTESIAN_POINT('Ctrl Pts',(19.0805109637125,21.7474404491387,5.25064418913795));
#138670=CARTESIAN_POINT('Ctrl Pts',(19.1637358812804,21.7360708361044,5.2548153031159));
#138671=CARTESIAN_POINT('Ctrl Pts',(19.2464624890053,21.72059234168,5.25898641709386));
#138672=CARTESIAN_POINT('Ctrl Pts',(19.328257802176,21.7010718191556,5.26315753107181));
#138673=CARTESIAN_POINT('Ctrl Pts',(19.4100256681394,21.6815578469311,5.26732724539218));
#138674=CARTESIAN_POINT('Ctrl Pts',(19.4908624130938,21.658004647022,5.27149695971255));
#138675=CARTESIAN_POINT('Ctrl Pts',(19.570345761113,21.6305300717016,5.27566667403293));
#138676=CARTESIAN_POINT('Ctrl Pts',(19.6498262807736,21.6030564740445,5.27983623997697));
#138677=CARTESIAN_POINT('Ctrl Pts',(19.7279530647407,21.5716619295133,5.28400580592101));
#138678=CARTESIAN_POINT('Ctrl Pts',(19.8043208135646,21.5365135682362,5.28817537186506));
#138679=CARTESIAN_POINT('Ctrl Pts',(19.8833735582273,21.5001294339367,5.29249153460398));
#138680=CARTESIAN_POINT('Ctrl Pts',(19.9605407918122,21.4597228236284,5.2968076973429));
#138681=CARTESIAN_POINT('Ctrl Pts',(20.0353992838381,21.4155316745345,5.30112386008182));
#138682=CARTESIAN_POINT('Ctrl Pts',(20.1078192683599,21.3727800474742,5.3052994242735));
#138683=CARTESIAN_POINT('Ctrl Pts',(20.1780782485913,21.3264869565082,5.30947498846518));
#138684=CARTESIAN_POINT('Ctrl Pts',(20.2458229776825,21.2769117319361,5.31365055265686));
#138685=CARTESIAN_POINT('Ctrl Pts',(20.3169893319923,21.2248325806247,5.3180370146694));
#138686=CARTESIAN_POINT('Ctrl Pts',(20.3853803178148,21.169131389708,5.32242347668194));
#138687=CARTESIAN_POINT('Ctrl Pts',(20.450627895575,21.110154724643,5.32680993869448));
#138688=CARTESIAN_POINT('Ctrl Pts',(20.5158754733353,21.0511780595779,5.33119640070702));
#138689=CARTESIAN_POINT('Ctrl Pts',(20.577979287096,20.9889263848496,5.33558286271956));
#138690=CARTESIAN_POINT('Ctrl Pts',(20.6366195645772,20.923786849695,5.3399693247321));
#138691=CARTESIAN_POINT('Ctrl Pts',(20.6925617159657,20.8616444811129,5.34415395912515));
#138692=CARTESIAN_POINT('Ctrl Pts',(20.7455602793472,20.7966428559979,5.3483385935182));
#138693=CARTESIAN_POINT('Ctrl Pts',(20.7953091936644,20.7290923582294,5.35252322791124));
#138694=CARTESIAN_POINT('Ctrl Pts',(20.8449872965599,20.6616380102333,5.35670190599518));
#138695=CARTESIAN_POINT('Ctrl Pts',(20.891424667568,20.5916423631925,5.36088058407913));
#138696=CARTESIAN_POINT('Ctrl Pts',(20.9343537398779,20.5194507707229,5.36505926216307));
#138697=CARTESIAN_POINT('Ctrl Pts',(20.9780522849564,20.4459651958413,5.36931284004851));
#138698=CARTESIAN_POINT('Ctrl Pts',(21.0181151991572,20.3702045348864,5.37356641793394));
#138699=CARTESIAN_POINT('Ctrl Pts',(21.0543048298795,20.2925662237875,5.37781999581938));
#138700=CARTESIAN_POINT('Ctrl Pts',(21.0897928539919,20.216433082848,5.38199110979733));
#138701=CARTESIAN_POINT('Ctrl Pts',(21.1215562334332,20.1384948820618,5.38616222377528));
#138702=CARTESIAN_POINT('Ctrl Pts',(21.1494168148283,20.0591518794677,5.39033333775324));
#138703=CARTESIAN_POINT('Ctrl Pts',(21.1772680473363,19.9798355011845,5.39450305207361));
#138704=CARTESIAN_POINT('Ctrl Pts',(21.2012189304411,19.899115690981,5.39867276639398));
#138705=CARTESIAN_POINT('Ctrl Pts',(21.2211399893043,19.8174113072851,5.40284248071435));
#138706=CARTESIAN_POINT('Ctrl Pts',(21.2410603392908,19.7357098309817,5.40701204665839));
#138707=CARTESIAN_POINT('Ctrl Pts',(21.2569510420042,19.6530242979868,5.41118161260244));
#138708=CARTESIAN_POINT('Ctrl Pts',(21.2687332465284,19.5697859653663,5.41535117854648));
#138709=CARTESIAN_POINT('Ctrl Pts',(21.2809296988286,19.4836210756564,5.4196673412854));
#138710=CARTESIAN_POINT('Ctrl Pts',(21.2887232939913,19.3968643124031,5.42398350402433));
#138711=CARTESIAN_POINT('Ctrl Pts',(21.2920850129342,19.3100003363693,5.42829966676325));
#138712=CARTESIAN_POINT('Ctrl Pts',(21.2953372242362,19.2259659452185,5.43247523095493));
#138713=CARTESIAN_POINT('Ctrl Pts',(21.2944419142066,19.1418316894466,5.43665079514661));
#138714=CARTESIAN_POINT('Ctrl Pts',(21.2894259327675,19.0580349643244,5.44082635933829));
#138715=CARTESIAN_POINT('Ctrl Pts',(21.2841566060303,18.9700058658239,5.44521282135083));
#138716=CARTESIAN_POINT('Ctrl Pts',(21.2743394628619,18.8823498716688,5.44959928336337));
#138717=CARTESIAN_POINT('Ctrl Pts',(21.2600666971253,18.7955640342066,5.45398574537592));
#138718=CARTESIAN_POINT('Ctrl Pts',(21.2457939313886,18.7087781967445,5.45837220738846));
#138719=CARTESIAN_POINT('Ctrl Pts',(21.2270657409798,18.6228630666792,5.462758669401));
#138720=CARTESIAN_POINT('Ctrl Pts',(21.2040345704695,18.5382970784324,5.46714513141354));
#138721=CARTESIAN_POINT('Ctrl Pts',(21.1820669712702,18.4576363176228,5.47132902816127));
#138722=CARTESIAN_POINT('Ctrl Pts',(21.1561032921526,18.3779026599639,5.475512924909));
#138723=CARTESIAN_POINT('Ctrl Pts',(21.1262387968719,18.2995212351674,5.47969682165673));
#138724=CARTESIAN_POINT('Ctrl Pts',(21.0964141293854,18.2212443411597,5.48387513868927));
#138725=CARTESIAN_POINT('Ctrl Pts',(21.0626991366596,18.1443165254359,5.48805345572181));
#138726=CARTESIAN_POINT('Ctrl Pts',(21.0252393289081,18.0691495992624,5.49223177275434));
#138727=CARTESIAN_POINT('Ctrl Pts',(20.9878182356733,17.9940603577164,5.49640577151794));
#138728=CARTESIAN_POINT('Ctrl Pts',(20.9466602184269,17.9207288006228,5.50057977028155));
#138729=CARTESIAN_POINT('Ctrl Pts',(20.901959036502,17.8495472406105,5.50475376904515));
#138730=CARTESIAN_POINT('Ctrl Pts',(20.8572882174576,17.7784140300401,5.50892493265719));
#138731=CARTESIAN_POINT('Ctrl Pts',(20.8090792576707,17.7094283045818,5.51309609626923));
#138732=CARTESIAN_POINT('Ctrl Pts',(20.7575714330078,17.6429570619672,5.51726725988127));
#138733=CARTESIAN_POINT('Ctrl Pts',(20.7060846236992,17.5765129398283,5.52143672164546));
#138734=CARTESIAN_POINT('Ctrl Pts',(20.6513019074186,17.5125816237505,5.52560618340965));
#138735=CARTESIAN_POINT('Ctrl Pts',(20.5935045656374,17.4514992837814,5.52977564517384));
#138736=CARTESIAN_POINT('Ctrl Pts',(20.5356974931344,17.3904066600305,5.53394580890583));
#138737=CARTESIAN_POINT('Ctrl Pts',(20.4748750940599,17.3321643081518,5.53811597263781));
#138738=CARTESIAN_POINT('Ctrl Pts',(20.4113567585147,17.2770728285003,5.54228613636979));
#138739=CARTESIAN_POINT('Ctrl Pts',(20.3730381658033,17.2438378900763,5.54480186358799));
#138740=CARTESIAN_POINT('Ctrl Pts',(20.3337391477832,17.2117489416272,5.54731759080619));
#138741=CARTESIAN_POINT('Ctrl Pts',(20.2935357313021,17.1808649545431,5.54983331802439));
#138742=CARTESIAN_POINT('Ctrl Pts',(20.2917777939292,17.1831894823608,4.74997346808549));
#138743=CARTESIAN_POINT('Ctrl Pts',(19.8562818492272,16.8534337186942,4.77707101139245));
#138744=CARTESIAN_POINT('Ctrl Pts',(18.4733993778667,16.3463965487828,4.84656049025989));
#138745=CARTESIAN_POINT('Ctrl Pts',(16.5671405518731,17.3473640177625,4.94099937082189));
#138746=CARTESIAN_POINT('Ctrl Pts',(16.1797898343239,18.7088775035926,5.00834070807693));
#138747=CARTESIAN_POINT('Ctrl Pts',(16.1776748250889,19.2121940791439,5.0332901097715));
#138748=CARTESIAN_POINT('',(16.1737368487789,19.2101644346317,4.96670989022851));
#138749=CARTESIAN_POINT('Ctrl Pts',(20.2944552424269,17.1796893591269,4.68319930761182));
#138750=CARTESIAN_POINT('Ctrl Pts',(20.1770115575366,17.0876168239104,4.6906344874789));
#138751=CARTESIAN_POINT('Ctrl Pts',(19.3369083402612,16.541881966795,4.74046160290647));
#138752=CARTESIAN_POINT('Ctrl Pts',(17.2348043502142,16.5812273130942,4.8326806538945));
#138753=CARTESIAN_POINT('Ctrl Pts',(16.1917618195022,18.2701494080764,4.91974900156632));
#138754=CARTESIAN_POINT('Ctrl Pts',(16.169904976237,19.1644257529645,4.96442541367765));
#138755=CARTESIAN_POINT('Ctrl Pts',(16.170099683962,19.2101632476096,4.96670989022851));
#138756=CARTESIAN_POINT('Ctrl Pts',(16.1740001363332,19.210164520558,4.96670989022851));
#138757=CARTESIAN_POINT('Ctrl Pts',(16.1739730621524,19.2931227545131,4.97085977152528));
#138758=CARTESIAN_POINT('Ctrl Pts',(16.1779827035226,19.3762448671897,4.97500965282206));
#138759=CARTESIAN_POINT('Ctrl Pts',(16.1860506816107,19.4591013319584,4.97915953411883));
#138760=CARTESIAN_POINT('Ctrl Pts',(16.194107496698,19.5418431550195,4.98330367356457));
#138761=CARTESIAN_POINT('Ctrl Pts',(16.2062114544436,19.6243195978693,4.9874478130103));
#138762=CARTESIAN_POINT('Ctrl Pts',(16.2223321624273,19.7061006702712,4.99159195245604));
#138763=CARTESIAN_POINT('Ctrl Pts',(16.2384354396281,19.7877933155319,4.99573161098225));
#138764=CARTESIAN_POINT('Ctrl Pts',(16.2585467481878,19.8687916269891,4.99987126950846));
#138765=CARTESIAN_POINT('Ctrl Pts',(16.2825840079949,19.9486717658564,5.00401092803467));
#138766=CARTESIAN_POINT('Ctrl Pts',(16.3066073287287,20.0285055826754,5.00814818599591));
#138767=CARTESIAN_POINT('Ctrl Pts',(16.3345519481597,20.1072220663068,5.01228544395717));
#138768=CARTESIAN_POINT('Ctrl Pts',(16.3662852025772,20.1844097996554,5.01642270191841));
#138769=CARTESIAN_POINT('Ctrl Pts',(16.398009961529,20.2615768686959,5.02055885227397));
#138770=CARTESIAN_POINT('Ctrl Pts',(16.4335211635115,20.3372155671951,5.02469500262952));
#138771=CARTESIAN_POINT('Ctrl Pts',(16.4726375176033,20.4109332161453,5.02883115298508));
#138772=CARTESIAN_POINT('Ctrl Pts',(16.5117556109319,20.4846541428151,5.03296748724695));
#138773=CARTESIAN_POINT('Ctrl Pts',(16.5544789534247,20.5564534375443,5.03710382150882));
#138774=CARTESIAN_POINT('Ctrl Pts',(16.6005803897988,20.6259631680044,5.04124015577069));
#138775=CARTESIAN_POINT('Ctrl Pts',(16.6467285005472,20.6955432720456,5.04538067777221));
#138776=CARTESIAN_POINT('Ctrl Pts',(16.6962612737686,20.7628287929976,5.04952119977374));
#138777=CARTESIAN_POINT('Ctrl Pts',(16.7489086678718,20.827481488638,5.05366172177526));
#138778=CARTESIAN_POINT('Ctrl Pts',(16.8015842228015,20.8921687666805,5.0578044585212));
#138779=CARTESIAN_POINT('Ctrl Pts',(16.8573774008546,20.9542200685977,5.06194719526713));
#138780=CARTESIAN_POINT('Ctrl Pts',(16.9159800655225,21.0133327988588,5.06608993201307));
#138781=CARTESIAN_POINT('Ctrl Pts',(16.9746826938387,21.0725463628314,5.07023973538442));
#138782=CARTESIAN_POINT('Ctrl Pts',(17.0362040315226,21.1288110311767,5.07438953875576));
#138783=CARTESIAN_POINT('Ctrl Pts',(17.1002018437174,21.1818636646221,5.07853934212711));
#138784=CARTESIAN_POINT('Ctrl Pts',(17.1438608301668,21.2180559050325,5.08137031717053));
#138785=CARTESIAN_POINT('Ctrl Pts',(17.1886716656524,21.2527541562677,5.08420129221395));
#138786=CARTESIAN_POINT('Ctrl Pts',(17.2345184376715,21.2858867545572,5.08703226725736));
#138787=CARTESIAN_POINT('Ctrl Pts',(17.3022873074279,21.3348620398235,5.09121690165041));
#138788=CARTESIAN_POINT('Ctrl Pts',(17.3725842232475,21.38060482739,5.09540153604346));
#138789=CARTESIAN_POINT('Ctrl Pts',(17.4450678487464,21.4228440065847,5.09958617043651));
#138790=CARTESIAN_POINT('Ctrl Pts',(17.5174483027762,21.4650230635361,5.10376484852045));
#138791=CARTESIAN_POINT('Ctrl Pts',(17.5920088899904,21.5037081881329,5.10794352660439));
#138792=CARTESIAN_POINT('Ctrl Pts',(17.6683776217254,21.5386702831201,5.11212220468833));
#138793=CARTESIAN_POINT('Ctrl Pts',(17.7461152080915,21.5742590485331,5.11637578257377));
#138794=CARTESIAN_POINT('Ctrl Pts',(17.8257260077702,21.6059897185084,5.12062936045921));
#138795=CARTESIAN_POINT('Ctrl Pts',(17.9067894477689,21.6336685085413,5.12488293834464));
#138796=CARTESIAN_POINT('Ctrl Pts',(17.986281314801,21.6608106912186,5.12905405232259));
#138797=CARTESIAN_POINT('Ctrl Pts',(18.067169544845,21.6840565436589,5.13322516630055));
#138798=CARTESIAN_POINT('Ctrl Pts',(18.1490371223203,21.7032717411504,5.1373962802785));
#138799=CARTESIAN_POINT('Ctrl Pts',(18.2308772283394,21.7224804907968,5.14156599459888));
#138800=CARTESIAN_POINT('Ctrl Pts',(18.3136955816371,21.7376611666003,5.14573570891925));
#138801=CARTESIAN_POINT('Ctrl Pts',(18.3970618790072,21.7487298324727,5.14990542323963));
#138802=CARTESIAN_POINT('Ctrl Pts',(18.4804252098464,21.7597981044744,5.15407498918367));
#138803=CARTESIAN_POINT('Ctrl Pts',(18.5643359898475,21.7667545977695,5.15824455512771));
#138804=CARTESIAN_POINT('Ctrl Pts',(18.6483570024151,21.7695670358552,5.16241412107175));
#138805=CARTESIAN_POINT('Ctrl Pts',(18.7353320901336,21.7724783557944,5.16673028381067));
#138806=CARTESIAN_POINT('Ctrl Pts',(18.822424779069,21.7709487709588,5.17104644654959));
#138807=CARTESIAN_POINT('Ctrl Pts',(18.909150084646,21.7650012623036,5.17536260928851));
#138808=CARTESIAN_POINT('Ctrl Pts',(18.9930503225158,21.7592474931174,5.1795381734802));
#138809=CARTESIAN_POINT('Ctrl Pts',(19.076606282259,21.7493593099811,5.18371373767188));
#138810=CARTESIAN_POINT('Ctrl Pts',(19.1593859487961,21.735410187463,5.18788930186356));
#138811=CARTESIAN_POINT('Ctrl Pts',(19.2463466195001,21.7207565279273,5.1922757638761));
#138812=CARTESIAN_POINT('Ctrl Pts',(19.3324499449363,21.7016210383821,5.19666222588864));
#138813=CARTESIAN_POINT('Ctrl Pts',(19.4172115835233,21.6781485427796,5.20104868790118));
#138814=CARTESIAN_POINT('Ctrl Pts',(19.5019732221104,21.6546760471771,5.20543514991372));
#138815=CARTESIAN_POINT('Ctrl Pts',(19.5853926474676,21.6268668011754,5.20982161192626));
#138816=CARTESIAN_POINT('Ctrl Pts',(19.6670104728636,21.5949235427183,5.2142080739388));
#138817=CARTESIAN_POINT('Ctrl Pts',(19.7448729411266,21.5644500409342,5.21839270833185));
#138818=CARTESIAN_POINT('Ctrl Pts',(19.8213857737636,21.5301011627872,5.22257734272491));
#138819=CARTESIAN_POINT('Ctrl Pts',(19.8961362506934,21.4920171710937,5.22676197711796));
#138820=CARTESIAN_POINT('Ctrl Pts',(19.9707803295714,21.4539873872486,5.2309406552019));
#138821=CARTESIAN_POINT('Ctrl Pts',(20.0436666290094,21.4122332570929,5.23511933328584));
#138822=CARTESIAN_POINT('Ctrl Pts',(20.1144011640627,21.3669435582256,5.23929801136979));
#138823=CARTESIAN_POINT('Ctrl Pts',(20.1864035648208,21.3208420740552,5.24355158925522));
#138824=CARTESIAN_POINT('Ctrl Pts',(20.2561758527105,21.2710772000454,5.24780516714066));
#138825=CARTESIAN_POINT('Ctrl Pts',(20.3233274374462,21.217897679649,5.2520587450261));
#138826=CARTESIAN_POINT('Ctrl Pts',(20.3891771576762,21.1657491480268,5.25622985900405));
#138827=CARTESIAN_POINT('Ctrl Pts',(20.4525065055987,21.1103174864332,5.26040097298199));
#138828=CARTESIAN_POINT('Ctrl Pts',(20.5129768127641,21.0518806315586,5.26457208695994));
#138829=CARTESIAN_POINT('Ctrl Pts',(20.5734268285339,20.993463385735,5.26874180128032));
#138830=CARTESIAN_POINT('Ctrl Pts',(20.6310193783563,20.9320432687884,5.27291151560069));
#138831=CARTESIAN_POINT('Ctrl Pts',(20.6854509703001,20.8679366646057,5.27708122992106));
#138832=CARTESIAN_POINT('Ctrl Pts',(20.7398806253343,20.8038323416111,5.28125079586511));
#138833=CARTESIAN_POINT('Ctrl Pts',(20.7911492490274,20.7370420726791,5.28542036180915));
#138834=CARTESIAN_POINT('Ctrl Pts',(20.8389930448979,20.6679160171168,5.2895899277532));
#138835=CARTESIAN_POINT('Ctrl Pts',(20.8885189696094,20.5963595747172,5.29390609049212));
#138836=CARTESIAN_POINT('Ctrl Pts',(20.9343744515018,20.5223004707788,5.29822225323104));
#138837=CARTESIAN_POINT('Ctrl Pts',(20.9763163009699,20.446158939734,5.30253841596996));
#138838=CARTESIAN_POINT('Ctrl Pts',(21.016891899103,20.3724977110544,5.30671398016164));
#138839=CARTESIAN_POINT('Ctrl Pts',(21.0538047581691,20.2968880859402,5.31088954435332));
#138840=CARTESIAN_POINT('Ctrl Pts',(21.0868828170839,20.2197330910957,5.31506510854501));
#138841=CARTESIAN_POINT('Ctrl Pts',(21.1216315701187,20.1386811808803,5.31945157055755));
#138842=CARTESIAN_POINT('Ctrl Pts',(21.1521477486479,20.0559242327775,5.32383803257009));
#138843=CARTESIAN_POINT('Ctrl Pts',(21.1782909617847,19.9719478918674,5.32822449458262));
#138844=CARTESIAN_POINT('Ctrl Pts',(21.2044341749215,19.8879715509573,5.33261095659516));
#138845=CARTESIAN_POINT('Ctrl Pts',(21.226204352714,19.8027763982256,5.3369974186077));
#138846=CARTESIAN_POINT('Ctrl Pts',(21.2435233083642,19.7168584434175,5.34138388062024));
#138847=CARTESIAN_POINT('Ctrl Pts',(21.2600453931921,19.6348937010711,5.34556851501329));
#138848=CARTESIAN_POINT('Ctrl Pts',(21.2725783676241,19.5519661209787,5.34975314940633));
#138849=CARTESIAN_POINT('Ctrl Pts',(21.2810167729394,19.4684986570166,5.35393778379938));
#138850=CARTESIAN_POINT('Ctrl Pts',(21.2894431672292,19.3851499986583,5.35811646188332));
#138851=CARTESIAN_POINT('Ctrl Pts',(21.2937865229904,19.3012634366145,5.36229513996726));
#138852=CARTESIAN_POINT('Ctrl Pts',(21.293992315731,19.2172724316077,5.36647381805121));
#138853=CARTESIAN_POINT('Ctrl Pts',(21.2942017971586,19.1317759481995,5.37072739593664));
#138854=CARTESIAN_POINT('Ctrl Pts',(21.290123829677,19.0461717133521,5.37498097382208));
#138855=CARTESIAN_POINT('Ctrl Pts',(21.2817561480521,18.9609227917969,5.37923455170752));
#138856=CARTESIAN_POINT('Ctrl Pts',(21.2735506902637,18.8773265869357,5.38340566568547));
#138857=CARTESIAN_POINT('Ctrl Pts',(21.2612204100085,18.7940725203434,5.38757677966342));
#138858=CARTESIAN_POINT('Ctrl Pts',(21.2448156932503,18.7115958004499,5.39174789364137));
#138859=CARTESIAN_POINT('Ctrl Pts',(21.2284164812531,18.6291467564163,5.39591760796174));
#138860=CARTESIAN_POINT('Ctrl Pts',(21.2079456377351,18.5474749918556,5.40008732228212));
#138861=CARTESIAN_POINT('Ctrl Pts',(21.1835049170498,18.4670069480508,5.40425703660249));
#138862=CARTESIAN_POINT('Ctrl Pts',(21.1590650660704,18.3865417676445,5.40842660254653));
#138863=CARTESIAN_POINT('Ctrl Pts',(21.1306557533066,18.3072806627591,5.41259616849058));
#138864=CARTESIAN_POINT('Ctrl Pts',(21.0984286192895,18.2296349790804,5.41676573443462));
#138865=CARTESIAN_POINT('Ctrl Pts',(21.0650684189969,18.1492593689498,5.42108189717354));
#138866=CARTESIAN_POINT('Ctrl Pts',(21.0276171353223,18.0706153771457,5.42539805991246));
#138867=CARTESIAN_POINT('Ctrl Pts',(20.9862964849992,17.9941349525685,5.42971422265138));
#138868=CARTESIAN_POINT('Ctrl Pts',(20.9463218505141,17.9201458697776,5.43388978684306));
#138869=CARTESIAN_POINT('Ctrl Pts',(20.9027263517805,17.8481819408653,5.43806535103475));
#138870=CARTESIAN_POINT('Ctrl Pts',(20.8557557370745,17.7786059926852,5.44224091522643));
#138871=CARTESIAN_POINT('Ctrl Pts',(20.8064127482817,17.7055159287636,5.44662737723897));
#138872=CARTESIAN_POINT('Ctrl Pts',(20.753345080151,17.6350618855121,5.45101383925151));
#138873=CARTESIAN_POINT('Ctrl Pts',(20.6968850924154,17.5676247799199,5.45540030126405));
#138874=CARTESIAN_POINT('Ctrl Pts',(20.6404251046797,17.5001876743276,5.45978676327659));
#138875=CARTESIAN_POINT('Ctrl Pts',(20.5805732479925,17.4357678796896,5.46417322528913));
#138876=CARTESIAN_POINT('Ctrl Pts',(20.5177042670235,17.3746996193972,5.46855968730167));
#138877=CARTESIAN_POINT('Ctrl Pts',(20.4577251723828,17.3164384720528,5.47274451766051));
#138878=CARTESIAN_POINT('Ctrl Pts',(20.3947769753971,17.2610106350633,5.47692934801934));
#138879=CARTESIAN_POINT('Ctrl Pts',(20.3291582734114,17.2087337632655,5.48111417837818));
#138880=CARTESIAN_POINT('Ctrl Pts',(20.3173695604846,17.1993419737956,5.48186600312105));
#138881=CARTESIAN_POINT('Ctrl Pts',(20.3054947581847,17.1900517964612,5.48261782786391));
#138882=CARTESIAN_POINT('Ctrl Pts',(20.2935357313021,17.1808649545431,5.48336965260678));
#138883=CARTESIAN_POINT('Origin',(18.734,19.211,-1.76670989022852));
#138884=CARTESIAN_POINT('',(20.295886890029,17.177834979693,6.34984102629757));
#138885=CARTESIAN_POINT('',(20.2935357313021,17.1808649545431,6.28334280090994));
#138886=CARTESIAN_POINT('',(20.2935357313021,17.1808649545432,-1.76670989022852));
#138887=CARTESIAN_POINT('',(16.1740005630998,19.2126979607665,5.83329010977151));
#138888=CARTESIAN_POINT('Ctrl Pts',(16.1712326816491,19.2126997966084,5.83329010977151));
#138889=CARTESIAN_POINT('Ctrl Pts',(16.1704460797826,19.3154768238875,5.83841759033362));
#138890=CARTESIAN_POINT('Ctrl Pts',(16.2227680075723,20.2671650151133,5.88593700645621));
#138891=CARTESIAN_POINT('Ctrl Pts',(17.4141948907083,21.935225591005,5.97584835813926));
#138892=CARTESIAN_POINT('Ctrl Pts',(20.3102571304128,21.7953188766137,6.10302416482072));
#138893=CARTESIAN_POINT('Ctrl Pts',(21.7315664652912,19.3340467278774,6.22768838754014));
#138894=CARTESIAN_POINT('Ctrl Pts',(20.9266954619927,17.6674200774838,6.30996067469909));
#138895=CARTESIAN_POINT('Ctrl Pts',(20.295886890029,17.177834979693,6.34984102629757));
#138896=CARTESIAN_POINT('Ctrl Pts',(20.2935357313021,17.1808649545431,5.54983331802439));
#138897=CARTESIAN_POINT('Ctrl Pts',(20.2268224860743,17.1296162999688,5.55400789674241));
#138898=CARTESIAN_POINT('Ctrl Pts',(20.1576175666066,17.0816880438637,5.55818247546043));
#138899=CARTESIAN_POINT('Ctrl Pts',(20.0862915869519,17.0373147735104,5.56235705417845));
#138900=CARTESIAN_POINT('Ctrl Pts',(20.0149229584389,16.9929149704781,5.56653412905591));
#138901=CARTESIAN_POINT('Ctrl Pts',(19.9414311470599,16.9520746080451,5.57071120393336));
#138902=CARTESIAN_POINT('Ctrl Pts',(19.8662111296425,16.9149821520917,5.57488827881081));
#138903=CARTESIAN_POINT('Ctrl Pts',(19.7908651648739,16.8778275890457,5.57907234772436));
#138904=CARTESIAN_POINT('Ctrl Pts',(19.713785638875,16.8444336437072,5.58325641663791));
#138905=CARTESIAN_POINT('Ctrl Pts',(19.6353868855367,16.8149403841761,5.58744048555146));
#138906=CARTESIAN_POINT('Ctrl Pts',(19.5924128561123,16.7987737469663,5.58973396973263));
#138907=CARTESIAN_POINT('Ctrl Pts',(19.549042711016,16.7837782504094,5.5920274539138));
#138908=CARTESIAN_POINT('Ctrl Pts',(19.5053461655915,16.7699704850561,5.59432093809498));
#138909=CARTESIAN_POINT('Ctrl Pts',(19.4256185318271,16.7447771786174,5.59850557248802));
#138910=CARTESIAN_POINT('Ctrl Pts',(19.3445069543662,16.7234471296282,5.60269020688107));
#138911=CARTESIAN_POINT('Ctrl Pts',(19.2624206826507,16.7061304261206,5.60687484127412));
#138912=CARTESIAN_POINT('Ctrl Pts',(19.1804512505827,16.688838370797,5.61105351935806));
#138913=CARTESIAN_POINT('Ctrl Pts',(19.097510326263,16.6755484082766,5.615232197442));
#138914=CARTESIAN_POINT('Ctrl Pts',(19.0140230530434,16.6663611081797,5.61941087552595));
#138915=CARTESIAN_POINT('Ctrl Pts',(18.9290393304527,16.6570091323315,5.62366445341138));
#138916=CARTESIAN_POINT('Ctrl Pts',(18.8434899394339,16.651908491303,5.62791803129682));
#138917=CARTESIAN_POINT('Ctrl Pts',(18.7578350465908,16.6511109612809,5.63217160918225));
#138918=CARTESIAN_POINT('Ctrl Pts',(18.6738407409873,16.6503288929346,5.6363427231602));
#138919=CARTESIAN_POINT('Ctrl Pts',(18.58974546897,16.6536845805936,5.64051383713816));
#138920=CARTESIAN_POINT('Ctrl Pts',(18.5059873315598,16.6611744720411,5.64468495111611));
#138921=CARTESIAN_POINT('Ctrl Pts',(18.4222573000016,16.6686618501832,5.64885466543648));
#138922=CARTESIAN_POINT('Ctrl Pts',(18.3388646361981,16.6802806360296,5.65302437975685));
#138923=CARTESIAN_POINT('Ctrl Pts',(18.2562442180638,16.6959752659613,5.65719409407722));
#138924=CARTESIAN_POINT('Ctrl Pts',(18.1736267399186,16.7116693374106,5.66136366002127));
#138925=CARTESIAN_POINT('Ctrl Pts',(18.0917819045974,16.7314388778862,5.66553322596531));
#138926=CARTESIAN_POINT('Ctrl Pts',(18.0111349162343,16.7551771092621,5.66970279190935));
#138927=CARTESIAN_POINT('Ctrl Pts',(17.9276524792492,16.7797499475688,5.67401895464827));
#138928=CARTESIAN_POINT('Ctrl Pts',(17.8454541950086,16.8085755987089,5.67833511738719));
#138929=CARTESIAN_POINT('Ctrl Pts',(17.7649932472178,16.8414798137466,5.68265128012612));
#138930=CARTESIAN_POINT('Ctrl Pts',(17.6871533063383,16.8733121774403,5.6868268443178));
#138931=CARTESIAN_POINT('Ctrl Pts',(17.6109396593042,16.9089612248341,5.69100240850947));
#138932=CARTESIAN_POINT('Ctrl Pts',(17.5367393343476,16.948221420801,5.69517797270115));
#138933=CARTESIAN_POINT('Ctrl Pts',(17.458791327372,16.989464555934,5.69956443471369));
#138934=CARTESIAN_POINT('Ctrl Pts',(17.3830658746254,17.0346929255447,5.70395089672624));
#138935=CARTESIAN_POINT('Ctrl Pts',(17.3099772536615,17.0836168145088,5.70833735873878));
#138936=CARTESIAN_POINT('Ctrl Pts',(17.2368886326976,17.1325407034729,5.71272382075132));
#138937=CARTESIAN_POINT('Ctrl Pts',(17.1664372628671,17.185159703645,5.71711028276386));
#138938=CARTESIAN_POINT('Ctrl Pts',(17.0989955289255,17.2411369642621,5.72149674477641));
#138939=CARTESIAN_POINT('Ctrl Pts',(17.0355419517776,17.2938040179914,5.72562381401755));
#138940=CARTESIAN_POINT('Ctrl Pts',(16.9745020021859,17.3496514870446,5.72975088325869));
#138941=CARTESIAN_POINT('Ctrl Pts',(16.9162185170908,17.4084267059583,5.73387795249983));
#138942=CARTESIAN_POINT('Ctrl Pts',(16.8577217299028,17.4674170265802,5.73802012571948));
#138943=CARTESIAN_POINT('Ctrl Pts',(16.8020020379166,17.5293563204315,5.74216229893914));
#138944=CARTESIAN_POINT('Ctrl Pts',(16.7493744028763,17.5939467419898,5.74630447215879));
#138945=CARTESIAN_POINT('Ctrl Pts',(16.6970742796338,17.658135205051,5.75042086784546));
#138946=CARTESIAN_POINT('Ctrl Pts',(16.6478281605157,17.7249415391099,5.75453726353214));
#138947=CARTESIAN_POINT('Ctrl Pts',(16.6019085746493,17.7940362905332,5.75865365921882));
#138948=CARTESIAN_POINT('Ctrl Pts',(16.5560170315912,17.8630888462173,5.76276754104799));
#138949=CARTESIAN_POINT('Ctrl Pts',(16.5134482524876,17.9344266527044,5.76688142287718));
#138950=CARTESIAN_POINT('Ctrl Pts',(16.4744330306067,18.0076891046671,5.77099530470636));
#138951=CARTESIAN_POINT('Ctrl Pts',(16.4354291736145,18.0809302157386,5.77510798818765));
#138952=CARTESIAN_POINT('Ctrl Pts',(16.3999770407451,18.1560944409467,5.77922067166894));
#138953=CARTESIAN_POINT('Ctrl Pts',(16.3682620211174,18.2327956168202,5.78333335515023));
#138954=CARTESIAN_POINT('Ctrl Pts',(16.3361584999703,18.3104363640294,5.78749641803534));
#138955=CARTESIAN_POINT('Ctrl Pts',(16.3078844956125,18.3896515290332,5.79165948092045));
#138956=CARTESIAN_POINT('Ctrl Pts',(16.2835818660733,18.4700202641616,5.79582254380555));
#138957=CARTESIAN_POINT('Ctrl Pts',(16.2595524301163,18.5494855487963,5.79993880837771));
#138958=CARTESIAN_POINT('Ctrl Pts',(16.2394055983611,18.6300781193828,5.80405507294986));
#138959=CARTESIAN_POINT('Ctrl Pts',(16.2232275631063,18.7113783730311,5.80817133752201));
#138960=CARTESIAN_POINT('Ctrl Pts',(16.2067736327736,18.7940650953989,5.81235779956359));
#138961=CARTESIAN_POINT('Ctrl Pts',(16.1944252132088,18.877483359597,5.81654426160518));
#138962=CARTESIAN_POINT('Ctrl Pts',(16.186218055036,18.9611857471735,5.82073072364676));
#138963=CARTESIAN_POINT('Ctrl Pts',(16.1780108968631,19.04488813475,5.82491718568835));
#138964=CARTESIAN_POINT('Ctrl Pts',(16.1739449655996,19.1288741338656,5.82910364772993));
#138965=CARTESIAN_POINT('Ctrl Pts',(16.1740005630998,19.2126979607665,5.83329010977151));
#138966=CARTESIAN_POINT('',(16.1740007055014,19.2090994299067,5.76670989019962));
#138967=CARTESIAN_POINT('Ctrl Pts',(20.2935357313021,17.1808649545431,5.48336965260678));
#138968=CARTESIAN_POINT('Ctrl Pts',(20.227081572348,17.1298153282562,5.48754740732368));
#138969=CARTESIAN_POINT('Ctrl Pts',(20.1580238969575,17.081959642987,5.49172516204058));
#138970=CARTESIAN_POINT('Ctrl Pts',(20.0867037125059,17.0375712189784,5.49590291675747));
#138971=CARTESIAN_POINT('Ctrl Pts',(20.0154603367112,16.9932305993224,5.50007617221891));
#138972=CARTESIAN_POINT('Ctrl Pts',(19.9419596834941,16.95235006111,5.50424942768034));
#138973=CARTESIAN_POINT('Ctrl Pts',(19.8665733319354,16.9151607966173,5.50842268314178));
#138974=CARTESIAN_POINT('Ctrl Pts',(19.7912312554809,16.877993373725,5.51259348761154));
#138975=CARTESIAN_POINT('Ctrl Pts',(19.7140060910258,16.8445131234673,5.5167642920813));
#138976=CARTESIAN_POINT('Ctrl Pts',(19.6352947388022,16.8149057210102,5.52093509655106));
#138977=CARTESIAN_POINT('Ctrl Pts',(19.5566060026711,16.7853068256329,5.52510470262571));
#138978=CARTESIAN_POINT('Ctrl Pts',(19.4764323572486,16.7595787296885,5.52927430870036));
#138979=CARTESIAN_POINT('Ctrl Pts',(19.3951901708556,16.737858767081,5.533443914775));
#138980=CARTESIAN_POINT('Ctrl Pts',(19.3139469571518,16.7161385298238,5.53761357357449));
#138981=CARTESIAN_POINT('Ctrl Pts',(19.2316356204149,16.6984266441197,5.54178323237398));
#138982=CARTESIAN_POINT('Ctrl Pts',(19.1486858298494,16.6848100501898,5.54595289117347));
#138983=CARTESIAN_POINT('Ctrl Pts',(19.0656524342559,16.6711797321056,5.55012675256875));
#138984=CARTESIAN_POINT('Ctrl Pts',(18.9819797544012,16.6616530259133,5.55430061396403));
#138985=CARTESIAN_POINT('Ctrl Pts',(18.8981052937467,16.6562652872432,5.55847447535931));
#138986=CARTESIAN_POINT('Ctrl Pts',(18.8141902295685,16.6508749403755,5.56265035731578));
#138987=CARTESIAN_POINT('Ctrl Pts',(18.7300736505504,16.6496275593595,5.56682623927225));
#138988=CARTESIAN_POINT('Ctrl Pts',(18.6461933267713,16.6525063048472,5.57100212122872));
#138989=CARTESIAN_POINT('Ctrl Pts',(18.5621614384985,16.6553902519792,5.57518554864289));
#138990=CARTESIAN_POINT('Ctrl Pts',(18.4783671181011,16.6624151854174,5.57936897605705));
#138991=CARTESIAN_POINT('Ctrl Pts',(18.3952432252439,16.6735122960777,5.58355240347122));
#138992=CARTESIAN_POINT('Ctrl Pts',(18.3145513419211,16.6842847313889,5.58761343364185));
#138993=CARTESIAN_POINT('Ctrl Pts',(18.2344915620021,16.6988941878814,5.59167446381248));
#138994=CARTESIAN_POINT('Ctrl Pts',(18.1554472698611,16.7172324209243,5.59573549398311));
#138995=CARTESIAN_POINT('Ctrl Pts',(18.073997132933,16.7361288086573,5.59992012837615));
#138996=CARTESIAN_POINT('Ctrl Pts',(17.9933221701874,16.7590549809083,5.6041047627692));
#138997=CARTESIAN_POINT('Ctrl Pts',(17.9138510440902,16.7859318174286,5.60828939716224));
#138998=CARTESIAN_POINT('Ctrl Pts',(17.834493035304,16.812770398099,5.6124680752462));
#138999=CARTESIAN_POINT('Ctrl Pts',(17.7563358916495,16.8435483273114,5.61664675333015));
#139000=CARTESIAN_POINT('Ctrl Pts',(17.6797967513069,16.8781357711078,5.6208254314141));
#139001=CARTESIAN_POINT('Ctrl Pts',(17.6018857018817,16.9133431699765,5.62507900929954));
#139002=CARTESIAN_POINT('Ctrl Pts',(17.525651701391,16.9524978888717,5.62933258718497));
#139003=CARTESIAN_POINT('Ctrl Pts',(17.4515171985762,16.9954102672083,5.63358616507041));
#139004=CARTESIAN_POINT('Ctrl Pts',(17.37881993776,17.0374907053542,5.63775727904836));
#139005=CARTESIAN_POINT('Ctrl Pts',(17.3081419118295,17.0831841629373,5.64192839302632));
#139006=CARTESIAN_POINT('Ctrl Pts',(17.2398584137959,17.1322645862507,5.64609950700427));
#139007=CARTESIAN_POINT('Ctrl Pts',(17.1715978289495,17.1813285401541,5.65026922132465));
#139008=CARTESIAN_POINT('Ctrl Pts',(17.1057305494611,17.2337769343488,5.65443893564503));
#139009=CARTESIAN_POINT('Ctrl Pts',(17.0426026198908,17.2893405862225,5.65860864996541));
#139010=CARTESIAN_POINT('Ctrl Pts',(16.9794769366831,17.344902260903,5.66277821590945));
#139011=CARTESIAN_POINT('Ctrl Pts',(16.9190907543423,17.4035786682715,5.66694778185349));
#139012=CARTESIAN_POINT('Ctrl Pts',(16.861755722101,17.4650614661809,5.67111734779753));
#139013=CARTESIAN_POINT('Ctrl Pts',(16.8024048608565,17.5287059234175,5.67543351053645));
#139014=CARTESIAN_POINT('Ctrl Pts',(16.7463240583274,17.5953574026467,5.67974967327537));
#139015=CARTESIAN_POINT('Ctrl Pts',(16.6938147044701,17.6646352435781,5.68406583601428));
#139016=CARTESIAN_POINT('Ctrl Pts',(16.6430158372917,17.731656366128,5.68824140020596));
#139017=CARTESIAN_POINT('Ctrl Pts',(16.5955595388125,17.8011349549808,5.69241696439764));
#139018=CARTESIAN_POINT('Ctrl Pts',(16.5516743299487,17.8726970933921,5.69659252858932));
#139019=CARTESIAN_POINT('Ctrl Pts',(16.5055725835125,17.9478736652917,5.70097899060186));
#139020=CARTESIAN_POINT('Ctrl Pts',(16.463412437974,18.0253492855826,5.7053654526144));
#139021=CARTESIAN_POINT('Ctrl Pts',(16.4254030213233,18.1046637084301,5.70975191462693));
#139022=CARTESIAN_POINT('Ctrl Pts',(16.3873936046726,18.1839781312776,5.71413837663947));
#139023=CARTESIAN_POINT('Ctrl Pts',(16.3535350701226,18.2651307919131,5.718524838652));
#139024=CARTESIAN_POINT('Ctrl Pts',(16.3239764935691,18.3476421955815,5.72291130066454));
#139025=CARTESIAN_POINT('Ctrl Pts',(16.2911969765864,18.4391447059584,5.72777574688621));
#139026=CARTESIAN_POINT('Ctrl Pts',(16.2636032939179,18.5325974942141,5.73264019310788));
#139027=CARTESIAN_POINT('Ctrl Pts',(16.2413973788042,18.6274486545232,5.73750463932955));
#139028=CARTESIAN_POINT('Ctrl Pts',(16.2191773325015,18.7223601753114,5.74237218114123));
#139029=CARTESIAN_POINT('Ctrl Pts',(16.2023520711405,18.818671733483,5.74723972295291));
#139030=CARTESIAN_POINT('Ctrl Pts',(16.191076093449,18.9158085274076,5.75210726476459));
#139031=CARTESIAN_POINT('Ctrl Pts',(16.1798001157575,19.0129453213322,5.75697480657626));
#139032=CARTESIAN_POINT('Ctrl Pts',(16.1740736044194,19.1109072194811,5.76184234838794));
#139033=CARTESIAN_POINT('Ctrl Pts',(16.1740007055014,19.2090994299067,5.76670989019962));
#139034=CARTESIAN_POINT('Ctrl Pts',(16.174000705501,19.2090994304895,5.76670989022851));
#139035=CARTESIAN_POINT('Ctrl Pts',(16.1739381768052,19.293323351932,5.77088500205647));
#139036=CARTESIAN_POINT('Ctrl Pts',(16.1780364138872,19.3775880720651,5.77506011388443));
#139037=CARTESIAN_POINT('Ctrl Pts',(16.1862808495761,19.4614538491682,5.77923522571239));
#139038=CARTESIAN_POINT('Ctrl Pts',(16.1945245019763,19.5453116583386,5.78340994087067));
#139039=CARTESIAN_POINT('Ctrl Pts',(16.2069135252696,19.6287701442273,5.78758465602896));
#139040=CARTESIAN_POINT('Ctrl Pts',(16.223381442754,19.7113943045357,5.79175937118724));
#139041=CARTESIAN_POINT('Ctrl Pts',(16.2398526754153,19.7940350980167,5.79593492676263));
#139042=CARTESIAN_POINT('Ctrl Pts',(16.2604043427346,19.8758407835677,5.80011048233803));
#139043=CARTESIAN_POINT('Ctrl Pts',(16.2849190524509,19.9563874914111,5.80428603791342));
#139044=CARTESIAN_POINT('Ctrl Pts',(16.3094630809744,20.0370305305357,5.80846658731946));
#139045=CARTESIAN_POINT('Ctrl Pts',(16.3379794801115,20.1164111473512,5.8126471367255));
#139046=CARTESIAN_POINT('Ctrl Pts',(16.3703013760236,20.1941219736187,5.81682768613154));
#139047=CARTESIAN_POINT('Ctrl Pts',(16.4026440716426,20.2718828081661,5.82101092579446));
#139048=CARTESIAN_POINT('Ctrl Pts',(16.4387969424261,20.3479712998167,5.82519416545737));
#139049=CARTESIAN_POINT('Ctrl Pts',(16.4785465454201,20.4220035979401,5.82937740512028));
#139050=CARTESIAN_POINT('Ctrl Pts',(16.5183679957904,20.4961697093842,5.83356820598561));
#139051=CARTESIAN_POINT('Ctrl Pts',(16.5617989238518,20.5682718138333,5.83775900685093));
#139052=CARTESIAN_POINT('Ctrl Pts',(16.6085819963923,20.6379542073733,5.84194980771626));
#139053=CARTESIAN_POINT('Ctrl Pts',(16.6388616407129,20.6830550948785,5.84466224092616));
#139054=CARTESIAN_POINT('Ctrl Pts',(16.6705446814796,20.7271429654286,5.84737467413607));
#139055=CARTESIAN_POINT('Ctrl Pts',(16.7035527014987,20.770129169764,5.85008710734598));
#139056=CARTESIAN_POINT('Ctrl Pts',(16.754476165831,20.8364465811684,5.85427174173903));
#139057=CARTESIAN_POINT('Ctrl Pts',(16.8087468503131,20.900389929485,5.85845637613207));
#139058=CARTESIAN_POINT('Ctrl Pts',(16.8661152556941,20.961601777101,5.86264101052512));
#139059=CARTESIAN_POINT('Ctrl Pts',(16.9234020042507,21.0227264972284,5.86681968860905));
#139060=CARTESIAN_POINT('Ctrl Pts',(16.9837774037101,21.0811271065649,5.87099836669299));
#139061=CARTESIAN_POINT('Ctrl Pts',(17.0469505633852,21.136477654614,5.87517704477692));
#139062=CARTESIAN_POINT('Ctrl Pts',(17.111256056546,21.1928203214572,5.87943062266236));
#139063=CARTESIAN_POINT('Ctrl Pts',(17.1784603025297,21.2460021244009,5.88368420054779));
#139064=CARTESIAN_POINT('Ctrl Pts',(17.2482157539318,21.2957170489387,5.88793777843323));
#139065=CARTESIAN_POINT('Ctrl Pts',(17.3166188597919,21.3444681526536,5.89210889241118));
#139066=CARTESIAN_POINT('Ctrl Pts',(17.3874747417492,21.3898853234966,5.89628000638914));
#139067=CARTESIAN_POINT('Ctrl Pts',(17.4604222489451,21.4317205389283,5.90045112036709));
#139068=CARTESIAN_POINT('Ctrl Pts',(17.5333452779005,21.4735417161494,5.90462083468746));
#139069=CARTESIAN_POINT('Ctrl Pts',(17.6083581394472,21.5117830963984,5.90879054900783));
#139070=CARTESIAN_POINT('Ctrl Pts',(17.6850725337908,21.546241137577,5.91296026332821));
#139071=CARTESIAN_POINT('Ctrl Pts',(17.761784198307,21.5806979525906,5.91712982927225));
#139072=CARTESIAN_POINT('Ctrl Pts',(17.8401968552426,21.6113715084925,5.92129939521629));
#139073=CARTESIAN_POINT('Ctrl Pts',(17.919900799999,21.6381057852013,5.92546896116033));
#139074=CARTESIAN_POINT('Ctrl Pts',(18.0024070371278,21.665780006099,5.92978512389925));
#139075=CARTESIAN_POINT('Ctrl Pts',(18.086296554875,21.6892326159301,5.93410128663818));
#139076=CARTESIAN_POINT('Ctrl Pts',(18.1710980677298,21.708346875115,5.9384174493771));
#139077=CARTESIAN_POINT('Ctrl Pts',(18.2531371802228,21.7268384893173,5.94259301356878));
#139078=CARTESIAN_POINT('Ctrl Pts',(18.3360293116296,21.7412700216398,5.94676857776046));
#139079=CARTESIAN_POINT('Ctrl Pts',(18.4193394847877,21.7515882704929,5.95094414195214));
#139080=CARTESIAN_POINT('Ctrl Pts',(18.5068574567409,21.7624276695664,5.95533060396469));
#139081=CARTESIAN_POINT('Ctrl Pts',(18.5948362284715,21.7687272994046,5.95971706597723));
#139082=CARTESIAN_POINT('Ctrl Pts',(18.6827702698546,21.7704873538952,5.96410352798978));
#139083=CARTESIAN_POINT('Ctrl Pts',(18.7707043112377,21.7722474083857,5.96848999000232));
#139084=CARTESIAN_POINT('Ctrl Pts',(18.8585930447506,21.7694679818952,5.97287645201486));
#139085=CARTESIAN_POINT('Ctrl Pts',(18.945938282031,21.7622119011579,5.97726291402741));
#139086=CARTESIAN_POINT('Ctrl Pts',(19.0292646354674,21.7552896834514,5.98144754842045));
#139087=CARTESIAN_POINT('Ctrl Pts',(19.1124065643326,21.7442679479863,5.9856321828135));
#139088=CARTESIAN_POINT('Ctrl Pts',(19.1949284709476,21.7291630099479,5.98981681720655));
#139089=CARTESIAN_POINT('Ctrl Pts',(19.2773329178427,21.7140795719192,5.99399549529049));
#139090=CARTESIAN_POINT('Ctrl Pts',(19.3591186468155,21.6949245577666,5.99817417337443));
#139091=CARTESIAN_POINT('Ctrl Pts',(19.4398541314692,21.6717661297018,6.00235285145837));
#139092=CARTESIAN_POINT('Ctrl Pts',(19.5220367416618,21.6481926034576,6.00660642934381));
#139093=CARTESIAN_POINT('Ctrl Pts',(19.6031306054563,21.6204707691485,6.01086000722925));
#139094=CARTESIAN_POINT('Ctrl Pts',(19.6826902922624,21.5887272192931,6.01511358511469));
#139095=CARTESIAN_POINT('Ctrl Pts',(19.7607075592917,21.557599080094,6.01928469909264));
#139096=CARTESIAN_POINT('Ctrl Pts',(19.8372491575629,21.5226039497269,6.02345581307059));
#139097=CARTESIAN_POINT('Ctrl Pts',(19.9119110552608,21.483911249014,6.02762692704854));
#139098=CARTESIAN_POINT('Ctrl Pts',(19.986547899438,21.4452315320104,6.03179664136892));
#139099=CARTESIAN_POINT('Ctrl Pts',(20.0593058876217,21.4028569203159,6.0359663556893));
#139100=CARTESIAN_POINT('Ctrl Pts',(20.1298036938044,21.3570037391305,6.04013607000967));
#139101=CARTESIAN_POINT('Ctrl Pts',(20.2002989913724,21.3111521895982,6.04430563595371));
#139102=CARTESIAN_POINT('Ctrl Pts',(20.268533881676,21.261822568227,6.04847520189775));
#139103=CARTESIAN_POINT('Ctrl Pts',(20.3341554111888,21.2092749210364,6.05264476784179));
#139104=CARTESIAN_POINT('Ctrl Pts',(20.4020841127265,21.154879763395,6.05696093058072));
#139105=CARTESIAN_POINT('Ctrl Pts',(20.4672118510046,21.0970364076613,6.06127709331964));
#139106=CARTESIAN_POINT('Ctrl Pts',(20.5291853686023,21.036077941447,6.06559325605856));
#139107=CARTESIAN_POINT('Ctrl Pts',(20.5891401053827,20.9771051908579,6.06976882025024));
#139108=CARTESIAN_POINT('Ctrl Pts',(20.6461426787833,20.9152175410395,6.07394438444192));
#139109=CARTESIAN_POINT('Ctrl Pts',(20.6999129097985,20.8507519419374,6.0781199486336));
#139110=CARTESIAN_POINT('Ctrl Pts',(20.7563989473557,20.7830303386772,6.08250641064614));
#139111=CARTESIAN_POINT('Ctrl Pts',(20.8093171796001,20.7124639847438,6.08689287265868));
#139112=CARTESIAN_POINT('Ctrl Pts',(20.8583941356916,20.639478055918,6.09127933467122));
#139113=CARTESIAN_POINT('Ctrl Pts',(20.9074710917831,20.5664921270922,6.09566579668377));
#139114=CARTESIAN_POINT('Ctrl Pts',(20.9527065384673,20.4910871600582,6.10005225869631));
#139115=CARTESIAN_POINT('Ctrl Pts',(20.9938836431733,20.4137160593082,6.10443872070885));
#139116=CARTESIAN_POINT('Ctrl Pts',(21.0331661282527,20.3399049175952,6.1086233551019));
#139117=CARTESIAN_POINT('Ctrl Pts',(21.0689017421373,20.2640298565515,6.11280798949495));
#139118=CARTESIAN_POINT('Ctrl Pts',(21.1008684225542,20.1864659759907,6.116992623888));
#139119=CARTESIAN_POINT('Ctrl Pts',(21.1327896023583,20.1090124980135,6.12117130197194));
#139120=CARTESIAN_POINT('Ctrl Pts',(21.1609523307067,20.0298753969623,6.12534998005588));
#139121=CARTESIAN_POINT('Ctrl Pts',(21.1851803441783,19.9494544131589,6.12952865813983));
#139122=CARTESIAN_POINT('Ctrl Pts',(21.2098426273791,19.8675919410183,6.13378223602526));
#139123=CARTESIAN_POINT('Ctrl Pts',(21.2304275222057,19.7843995318239,6.13803581391069));
#139124=CARTESIAN_POINT('Ctrl Pts',(21.2468003698023,19.7003202443407,6.14228939179613));
#139125=CARTESIAN_POINT('Ctrl Pts',(21.2628557977991,19.6178709979127,6.14646050577408));
#139126=CARTESIAN_POINT('Ctrl Pts',(21.2748609466778,19.5345694264046,6.15063161975203));
#139127=CARTESIAN_POINT('Ctrl Pts',(21.2827395777799,19.4508469609113,6.15480273372998));
#139128=CARTESIAN_POINT('Ctrl Pts',(21.2906155651312,19.3671525892999,6.15897244805035));
#139129=CARTESIAN_POINT('Ctrl Pts',(21.2943677416632,19.2830380618266,6.16314216237073));
#139130=CARTESIAN_POINT('Ctrl Pts',(21.2939715980996,19.1989411060454,6.1673118766911));
#139131=CARTESIAN_POINT('Ctrl Pts',(21.2935754686325,19.1148471427948,6.17148144263515));
#139132=CARTESIAN_POINT('Ctrl Pts',(21.2890313155854,19.0307712100168,6.1756510085792));
#139133=CARTESIAN_POINT('Ctrl Pts',(21.2803667494581,18.9471508437492,6.17982057452325));
#139134=CARTESIAN_POINT('Ctrl Pts',(21.2713975478746,18.8605904885606,6.18413673726217));
#139135=CARTESIAN_POINT('Ctrl Pts',(21.2580128490967,18.7745188559842,6.18845290000109));
#139136=CARTESIAN_POINT('Ctrl Pts',(21.2403015155518,18.6894132736132,6.19276906274001));
#139137=CARTESIAN_POINT('Ctrl Pts',(21.2231671268342,18.6070799966365,6.19694462693169));
#139138=CARTESIAN_POINT('Ctrl Pts',(21.2019838191122,18.5256512422048,6.20112019112337));
#139139=CARTESIAN_POINT('Ctrl Pts',(21.1768832583851,18.4455449811374,6.20529575531505));
#139140=CARTESIAN_POINT('Ctrl Pts',(21.1505149280066,18.3613927432581,6.20968221732759));
#139141=CARTESIAN_POINT('Ctrl Pts',(21.1198234271564,18.2787006554451,6.21406867934013));
#139142=CARTESIAN_POINT('Ctrl Pts',(21.0850182368018,18.1979288029831,6.21845514135267));
#139143=CARTESIAN_POINT('Ctrl Pts',(21.0502130464472,18.117156950521,6.22284160336521));
#139144=CARTESIAN_POINT('Ctrl Pts',(21.0112944915984,18.0383058200372,6.22722806537774));
#139145=CARTESIAN_POINT('Ctrl Pts',(20.9685260259017,17.9618028820206,6.23161452739028));
#139146=CARTESIAN_POINT('Ctrl Pts',(20.9264963505572,17.8866214698433,6.23592521685025));
#139147=CARTESIAN_POINT('Ctrl Pts',(20.880587598457,17.8134194333577,6.24023590631023));
#139148=CARTESIAN_POINT('Ctrl Pts',(20.8310139328075,17.7426224717018,6.2445465957702));
#139149=CARTESIAN_POINT('Ctrl Pts',(20.7829662991437,17.6740048612509,6.24872458876905));
#139150=CARTESIAN_POINT('Ctrl Pts',(20.7314763614704,17.6076468441108,6.25290258176791));
#139151=CARTESIAN_POINT('Ctrl Pts',(20.6767860578329,17.5439120198711,6.25708057476676));
#139152=CARTESIAN_POINT('Ctrl Pts',(20.6194902413024,17.4771407907252,6.26145761245729));
#139153=CARTESIAN_POINT('Ctrl Pts',(20.5586817691827,17.4132493747021,6.26583465014782));
#139154=CARTESIAN_POINT('Ctrl Pts',(20.4946892530986,17.3526207722795,6.27021168783835));
#139155=CARTESIAN_POINT('Ctrl Pts',(20.4306967370146,17.2919921698569,6.27458872552888));
#139156=CARTESIAN_POINT('Ctrl Pts',(20.3635205634202,17.2346268195884,6.27896576321941));
#139157=CARTESIAN_POINT('Ctrl Pts',(20.2935357313021,17.1808649545431,6.28334280090994));
#139158=CARTESIAN_POINT('Origin',(18.734,19.211,-1.76670989022852));
#139159=CARTESIAN_POINT('',(20.2935357313021,17.1808649545432,7.14996298022642));
#139160=CARTESIAN_POINT('',(20.2935357313021,17.1808649545432,7.08324142743447));
#139161=CARTESIAN_POINT('',(20.2935357313021,17.1808649545432,-1.76670989022852));
#139162=CARTESIAN_POINT('',(16.1740008768645,19.208881145288,6.6332901097715));
#139163=CARTESIAN_POINT('Ctrl Pts',(16.1740008768645,19.208881145288,6.6332901097715));
#139164=CARTESIAN_POINT('Ctrl Pts',(16.1739325519701,19.291431245901,6.63740642252224));
#139165=CARTESIAN_POINT('Ctrl Pts',(16.1778613169669,19.3741241408158,6.64152273527298));
#139166=CARTESIAN_POINT('Ctrl Pts',(16.1858020059738,19.456534077555,6.64563904802372));
#139167=CARTESIAN_POINT('Ctrl Pts',(16.1937337220434,19.5388508914938,6.64975070936243));
#139168=CARTESIAN_POINT('Ctrl Pts',(16.2056683130375,19.6208849121504,6.65386237070114));
#139169=CARTESIAN_POINT('Ctrl Pts',(16.2215685692311,19.7022110602219,6.65797403203985));
#139170=CARTESIAN_POINT('Ctrl Pts',(16.2374592000151,19.7834879765409,6.66208320433539));
#139171=CARTESIAN_POINT('Ctrl Pts',(16.2573106430752,19.8640574053625,6.66619237663093));
#139172=CARTESIAN_POINT('Ctrl Pts',(16.2810340922892,19.9435013690146,6.67030154892647));
#139173=CARTESIAN_POINT('Ctrl Pts',(16.3047507902537,20.0229227244023,6.67440955182852));
#139174=CARTESIAN_POINT('Ctrl Pts',(16.3323371713261,20.1012187954775,6.67851755473057));
#139175=CARTESIAN_POINT('Ctrl Pts',(16.3636541468012,20.1779852823199,6.68262555763262));
#139176=CARTESIAN_POINT('Ctrl Pts',(16.3949722554066,20.2547545467753,6.68673370917299));
#139177=CARTESIAN_POINT('Ctrl Pts',(16.4300210447236,20.3299936782016,6.69084186071336));
#139178=CARTESIAN_POINT('Ctrl Pts',(16.4686133150906,20.4033184003592,6.69495001225373));
#139179=CARTESIAN_POINT('Ctrl Pts',(16.5072438266208,20.4767157801408,6.69906223457025));
#139180=CARTESIAN_POINT('Ctrl Pts',(16.5494246053548,20.5481945435127,6.70317445688677));
#139181=CARTESIAN_POINT('Ctrl Pts',(16.5949228757402,20.6173957680782,6.70728667920329));
#139182=CARTESIAN_POINT('Ctrl Pts',(16.6404458510681,20.6866345679682,6.71140113440064));
#139183=CARTESIAN_POINT('Ctrl Pts',(16.6892896206456,20.7535929860938,6.715515589598));
#139184=CARTESIAN_POINT('Ctrl Pts',(16.7411800554792,20.8179438909682,6.71963004479535));
#139185=CARTESIAN_POINT('Ctrl Pts',(16.7931561866085,20.8824010704228,6.7237512949554));
#139186=CARTESIAN_POINT('Ctrl Pts',(16.8481887081045,20.9442417891331,6.72787254511546));
#139187=CARTESIAN_POINT('Ctrl Pts',(16.9059658904508,21.0031750177716,6.73199379527552));
#139188=CARTESIAN_POINT('Ctrl Pts',(16.9382542996129,21.0361094760171,6.73429692959297));
#139189=CARTESIAN_POINT('Ctrl Pts',(16.9713992632832,21.068136611825,6.73660006391043));
#139190=CARTESIAN_POINT('Ctrl Pts',(17.0053421035809,21.0992112903877,6.73890319822789));
#139191=CARTESIAN_POINT('Ctrl Pts',(17.067013876621,21.1556718136325,6.74308783262094));
#139192=CARTESIAN_POINT('Ctrl Pts',(17.1315694533286,21.2092127933028,6.74727246701399));
#139193=CARTESIAN_POINT('Ctrl Pts',(17.1987010234279,21.2595255801519,6.75145710140704));
#139194=CARTESIAN_POINT('Ctrl Pts',(17.2657370400465,21.3097667529765,6.75563577949099));
#139195=CARTESIAN_POINT('Ctrl Pts',(17.3353414020479,21.3567885864286,6.75981445757493));
#139196=CARTESIAN_POINT('Ctrl Pts',(17.4071710083241,21.4003206313485,6.76399313565888));
#139197=CARTESIAN_POINT('Ctrl Pts',(17.4802881086698,21.4446329568877,6.76824671354431));
#139198=CARTESIAN_POINT('Ctrl Pts',(17.5557106573434,21.4853288288425,6.77250029142975));
#139199=CARTESIAN_POINT('Ctrl Pts',(17.6330432222703,21.5221672751169,6.77675386931518));
#139200=CARTESIAN_POINT('Ctrl Pts',(17.7088765445241,21.5582915362259,6.78092498329313));
#139201=CARTESIAN_POINT('Ctrl Pts',(17.7865460506904,21.5907063974352,6.78509609727109));
#139202=CARTESIAN_POINT('Ctrl Pts',(17.8656529884827,21.6192303601585,6.78926721124904));
#139203=CARTESIAN_POINT('Ctrl Pts',(17.944733381178,21.6477447513906,6.79343692556941));
#139204=CARTESIAN_POINT('Ctrl Pts',(18.0252498151567,21.6723706812234,6.79760663988978));
#139205=CARTESIAN_POINT('Ctrl Pts',(18.1067845307987,21.6929751721551,6.80177635421015));
#139206=CARTESIAN_POINT('Ctrl Pts',(18.1883163450856,21.7135789298907,6.80594592015419));
#139207=CARTESIAN_POINT('Ctrl Pts',(18.2708659227709,21.7301614213603,6.81011548609824));
#139208=CARTESIAN_POINT('Ctrl Pts',(18.3540026821448,21.7426401873929,6.81428505204228));
#139209=CARTESIAN_POINT('Ctrl Pts',(18.440062427418,21.755557691445,6.8186012147812));
#139210=CARTESIAN_POINT('Ctrl Pts',(18.5267508916659,21.7640774486062,6.82291737752012));
#139211=CARTESIAN_POINT('Ctrl Pts',(18.6135836740996,21.7681663826307,6.82723354025904));
#139212=CARTESIAN_POINT('Ctrl Pts',(18.6975878877788,21.7721221200595,6.83140910445072));
#139213=CARTESIAN_POINT('Ctrl Pts',(18.7817266907701,21.7719313177434,6.83558466864241));
#139214=CARTESIAN_POINT('Ctrl Pts',(18.8655624783157,21.7676171622477,6.83976023283409));
#139215=CARTESIAN_POINT('Ctrl Pts',(18.9536326121894,21.7630851090138,6.84414669484663));
#139216=CARTESIAN_POINT('Ctrl Pts',(19.0413677347566,21.7540022746856,6.84853315685917));
#139217=CARTESIAN_POINT('Ctrl Pts',(19.1282700391328,21.7404566879554,6.8529196188717));
#139218=CARTESIAN_POINT('Ctrl Pts',(19.215172343509,21.7269111012251,6.85730608088424));
#139219=CARTESIAN_POINT('Ctrl Pts',(19.3012412773527,21.7089029553709,6.86169254289678));
#139220=CARTESIAN_POINT('Ctrl Pts',(19.3859971465595,21.6865806835727,6.86607900490932));
#139221=CARTESIAN_POINT('Ctrl Pts',(19.4668532725857,21.6652854925895,6.87026363930237));
#139222=CARTESIAN_POINT('Ctrl Pts',(19.5468154727231,21.6399851855305,6.87444827369542));
#139223=CARTESIAN_POINT('Ctrl Pts',(19.6254576099359,21.6107715161422,6.87863290808846));
#139224=CARTESIAN_POINT('Ctrl Pts',(19.7039878098005,21.5815994287963,6.88281158617242));
#139225=CARTESIAN_POINT('Ctrl Pts',(19.7812012513675,21.5485252020902,6.88699026425637));
#139226=CARTESIAN_POINT('Ctrl Pts',(19.8566848155709,21.5116909407581,6.89116894234032));
#139227=CARTESIAN_POINT('Ctrl Pts',(19.9335213684134,21.474196451764,6.89542252022575));
#139228=CARTESIAN_POINT('Ctrl Pts',(20.0085649515612,21.4328059278375,6.89967609811119));
#139229=CARTESIAN_POINT('Ctrl Pts',(20.0813989057343,21.3877214311496,6.90392967599662));
#139230=CARTESIAN_POINT('Ctrl Pts',(20.1528208315821,21.3435109854051,6.90810078997458));
#139231=CARTESIAN_POINT('Ctrl Pts',(20.2221176306652,21.2957487717612,6.91227190395253));
#139232=CARTESIAN_POINT('Ctrl Pts',(20.2889208543458,21.2446718360445,6.91644301793048));
#139233=CARTESIAN_POINT('Ctrl Pts',(20.3557016615595,21.1936120396869,6.92061273225086));
#139234=CARTESIAN_POINT('Ctrl Pts',(20.4199901900087,21.1392400094635,6.92478244657123));
#139235=CARTESIAN_POINT('Ctrl Pts',(20.4814485012998,21.0818350369033,6.92895216089161));
#139236=CARTESIAN_POINT('Ctrl Pts',(20.5429046256403,21.0244321070585,6.93312172683565));
#139237=CARTESIAN_POINT('Ctrl Pts',(20.6015303974546,20.9639967640997,6.93729129277969));
#139238=CARTESIAN_POINT('Ctrl Pts',(20.6570234159162,20.9008464255186,6.94146085872373));
#139239=CARTESIAN_POINT('Ctrl Pts',(20.7144675004488,20.8354757989374,6.94577702146265));
#139240=CARTESIAN_POINT('Ctrl Pts',(20.7685540894612,20.7671961022132,6.95009318420157));
#139241=CARTESIAN_POINT('Ctrl Pts',(20.8189931741053,20.6963967362069,6.95440934694048));
#139242=CARTESIAN_POINT('Ctrl Pts',(20.8677892108724,20.6279036521016,6.95858491113216));
#139243=CARTESIAN_POINT('Ctrl Pts',(20.9131715145603,20.5570529563654,6.96276047532384));
#139244=CARTESIAN_POINT('Ctrl Pts',(20.9549227142452,20.4842251557952,6.96693603951552));
#139245=CARTESIAN_POINT('Ctrl Pts',(20.9987826677721,20.40771899615,6.97132250152806));
#139246=CARTESIAN_POINT('Ctrl Pts',(21.0386347993092,20.3290312765029,6.97570896354059));
#139247=CARTESIAN_POINT('Ctrl Pts',(21.0742836736309,20.2486282219257,6.98009542555313));
#139248=CARTESIAN_POINT('Ctrl Pts',(21.1099325479526,20.1682251673484,6.98448188756567));
#139249=CARTESIAN_POINT('Ctrl Pts',(21.1413780286032,20.0861073468905,6.98886834957821));
#139250=CARTESIAN_POINT('Ctrl Pts',(21.1684852750765,20.0027584514458,6.99325481159075));
#139251=CARTESIAN_POINT('Ctrl Pts',(21.1943452769569,19.9232445622332,6.99743944598379));
#139252=CARTESIAN_POINT('Ctrl Pts',(21.2163537449119,19.8423144298574,7.00162408037684));
#139253=CARTESIAN_POINT('Ctrl Pts',(21.234357169427,19.7603760326908,7.00580871476988));
#139254=CARTESIAN_POINT('Ctrl Pts',(21.2523349682956,19.6785542646905,7.00998739285382));
#139255=CARTESIAN_POINT('Ctrl Pts',(21.2663189491972,19.5957275280112,7.01416607093776));
#139256=CARTESIAN_POINT('Ctrl Pts',(21.2762049862094,19.5123201090074,7.0183447490217));
#139257=CARTESIAN_POINT('Ctrl Pts',(21.2862682233301,19.4274176719616,7.02259832690714));
#139258=CARTESIAN_POINT('Ctrl Pts',(21.2920850111441,19.3419139888707,7.02685190479258));
#139259=CARTESIAN_POINT('Ctrl Pts',(21.2935997221946,19.2562687766721,7.03110548267801));
#139260=CARTESIAN_POINT('Ctrl Pts',(21.2950850676157,19.1722839640349,7.03527659665597));
#139261=CARTESIAN_POINT('Ctrl Pts',(21.2924336475013,19.0881635420989,7.03944771063392));
#139262=CARTESIAN_POINT('Ctrl Pts',(21.2856453456188,19.0043456262701,7.04361882461187));
#139263=CARTESIAN_POINT('Ctrl Pts',(21.2788593216167,18.9205558363527,7.04778853893224));
#139264=CARTESIAN_POINT('Ctrl Pts',(21.2679392098804,18.8370688090943,7.05195825325261));
#139265=CARTESIAN_POINT('Ctrl Pts',(21.252936930744,18.7543198724119,7.05612796757298));
#139266=CARTESIAN_POINT('Ctrl Pts',(21.2379351854531,18.6715738802916,7.06029753351702));
#139267=CARTESIAN_POINT('Ctrl Pts',(21.2188516444825,18.5895663790286,7.06446709946107));
#139268=CARTESIAN_POINT('Ctrl Pts',(21.1957895218785,18.5087234519298,7.06863666540511));
#139269=CARTESIAN_POINT('Ctrl Pts',(21.1719165634939,18.4250381872448,7.07295282814404));
#139270=CARTESIAN_POINT('Ctrl Pts',(21.1437801888442,18.3426014204637,7.07726899088296));
#139271=CARTESIAN_POINT('Ctrl Pts',(21.1115508461405,18.261867778433,7.08158515362188));
#139272=CARTESIAN_POINT('Ctrl Pts',(21.0803713708855,18.1837640263,7.08576071781356));
#139273=CARTESIAN_POINT('Ctrl Pts',(21.0453617283798,18.1072545529914,7.08993628200523));
#139274=CARTESIAN_POINT('Ctrl Pts',(21.006724205865,18.032728094167,7.09411184619691));
#139275=CARTESIAN_POINT('Ctrl Pts',(20.9661351939398,17.9544374810769,7.09849830820946));
#139276=CARTESIAN_POINT('Ctrl Pts',(20.9215424772638,17.8783359749763,7.102884770222));
#139277=CARTESIAN_POINT('Ctrl Pts',(20.8732322919594,17.8048402647501,7.10727123223455));
#139278=CARTESIAN_POINT('Ctrl Pts',(20.8249221066551,17.731344554524,7.11165769424709));
#139279=CARTESIAN_POINT('Ctrl Pts',(20.7728948573422,17.6604550629257,7.11604415625964));
#139280=CARTESIAN_POINT('Ctrl Pts',(20.7174842649081,17.5925469821889,7.12043061827219));
#139281=CARTESIAN_POINT('Ctrl Pts',(20.6646206180318,17.5277602935357,7.12461545674226));
#139282=CARTESIAN_POINT('Ctrl Pts',(20.6084810526672,17.4654457911788,7.12880029521234));
#139283=CARTESIAN_POINT('Ctrl Pts',(20.5493255613627,17.4059534337688,7.13298513368241));
#139284=CARTESIAN_POINT('Ctrl Pts',(20.4902614757737,17.346553002592,7.13716350583555));
#139285=CARTESIAN_POINT('Ctrl Pts',(20.428191047079,17.2899663736458,7.1413418779887));
#139286=CARTESIAN_POINT('Ctrl Pts',(20.3634146060967,17.2365106884466,7.14552025014184));
#139287=CARTESIAN_POINT('Ctrl Pts',(20.340456363622,17.2175647790412,7.14700116017003));
#139288=CARTESIAN_POINT('Ctrl Pts',(20.3171585650168,17.199011852374,7.14848207019823));
#139289=CARTESIAN_POINT('Ctrl Pts',(20.2935357313021,17.1808649545431,7.14996298022642));
#139290=CARTESIAN_POINT('Ctrl Pts',(20.295886890029,17.177834979693,6.34984102629757));
#139291=CARTESIAN_POINT('Ctrl Pts',(20.2561598407695,17.1470018994828,6.35235261025957));
#139292=CARTESIAN_POINT('Ctrl Pts',(19.528831972149,16.618320657574,6.39725612978206));
#139293=CARTESIAN_POINT('Ctrl Pts',(17.5479307751794,16.4259451726882,6.48455158486501));
#139294=CARTESIAN_POINT('Ctrl Pts',(16.2478508564243,18.0710820233979,6.57652302872766));
#139295=CARTESIAN_POINT('Ctrl Pts',(16.1710772436132,19.0646440698247,6.62610253702982));
#139296=CARTESIAN_POINT('Ctrl Pts',(16.172362658312,19.2088797893707,6.6332901097715));
#139297=CARTESIAN_POINT('',(16.174000571626,19.2127107672549,6.56670989025839));
#139298=CARTESIAN_POINT('Ctrl Pts',(20.2935357313021,17.1808649545431,6.28334280090994));
#139299=CARTESIAN_POINT('Ctrl Pts',(20.2268670407022,17.1296505265265,6.28751243828281));
#139300=CARTESIAN_POINT('Ctrl Pts',(20.1576502146725,17.081706158595,6.29168207565569));
#139301=CARTESIAN_POINT('Ctrl Pts',(20.0862433688758,17.0372847768552,6.29585171302856));
#139302=CARTESIAN_POINT('Ctrl Pts',(20.0148367281774,16.9928635227047,6.30002133842519));
#139303=CARTESIAN_POINT('Ctrl Pts',(19.9412404714991,16.9519654765769,6.30419096382183));
#139304=CARTESIAN_POINT('Ctrl Pts',(19.8658401643204,16.9147992591171,6.30836058921847));
#139305=CARTESIAN_POINT('Ctrl Pts',(19.7898457625222,16.8773402013408,6.31256306795624));
#139306=CARTESIAN_POINT('Ctrl Pts',(19.7120191739364,16.8436722636366,6.31676554669401));
#139307=CARTESIAN_POINT('Ctrl Pts',(19.632777078394,16.8139602082248,6.32096802543178));
#139308=CARTESIAN_POINT('Ctrl Pts',(19.5540386541307,16.7844370058318,6.32514379276286));
#139309=CARTESIAN_POINT('Ctrl Pts',(19.473903125821,16.7588196266226,6.32931956009393));
#139310=CARTESIAN_POINT('Ctrl Pts',(19.3927942358925,16.7372194610769,6.33349532742501));
#139311=CARTESIAN_POINT('Ctrl Pts',(19.3109070940739,16.7154120387227,6.33771116186612));
#139312=CARTESIAN_POINT('Ctrl Pts',(19.2280282808171,16.6976994334045,6.34192699630724));
#139313=CARTESIAN_POINT('Ctrl Pts',(19.1446022295193,16.6841430968269,6.34614283074836));
#139314=CARTESIAN_POINT('Ctrl Pts',(19.0611761782215,16.6705867602493,6.35035866518948));
#139315=CARTESIAN_POINT('Ctrl Pts',(18.9772033685603,16.6611866814948,6.3545744996306));
#139316=CARTESIAN_POINT('Ctrl Pts',(18.8931294701917,16.6559505265619,6.35879033407172));
#139317=CARTESIAN_POINT('Ctrl Pts',(18.8096777759695,16.650753122744,6.36297496846477));
#139318=CARTESIAN_POINT('Ctrl Pts',(18.7258158815285,16.6496388297568,6.36715960285782));
#139319=CARTESIAN_POINT('Ctrl Pts',(18.6419771668654,16.6526544802975,6.37134423725087));
#139320=CARTESIAN_POINT('Ctrl Pts',(18.5582577862359,16.6556658384328,6.3755229153348));
#139321=CARTESIAN_POINT('Ctrl Pts',(18.4745619756522,16.6627954472227,6.37970159341873));
#139322=CARTESIAN_POINT('Ctrl Pts',(18.391326582379,16.6740382484444,6.38388027150266));
#139323=CARTESIAN_POINT('Ctrl Pts',(18.3065992545013,16.6854825687981,6.3881338493881));
#139324=CARTESIAN_POINT('Ctrl Pts',(18.2223494934534,16.7011890198916,6.39238742727354));
#139325=CARTESIAN_POINT('Ctrl Pts',(18.1390363521675,16.7210967372691,6.39664100515897));
#139326=CARTESIAN_POINT('Ctrl Pts',(18.0573383986977,16.7406185046986,6.40081211913692));
#139327=CARTESIAN_POINT('Ctrl Pts',(17.97654154071,16.7641799807697,6.40498323311487));
#139328=CARTESIAN_POINT('Ctrl Pts',(17.8970700591986,16.7916719374607,6.40915434709282));
#139329=CARTESIAN_POINT('Ctrl Pts',(17.8176252451105,16.8191546689601,6.41332406141319));
#139330=CARTESIAN_POINT('Ctrl Pts',(17.7395053586246,16.8505651114303,6.41749377573356));
#139331=CARTESIAN_POINT('Ctrl Pts',(17.6631189946712,16.8857443425666,6.42166349005393));
#139332=CARTESIAN_POINT('Ctrl Pts',(17.5867353488724,16.9209223218749,6.42583305599797));
#139333=CARTESIAN_POINT('Ctrl Pts',(17.5120855204511,16.959868629993,6.43000262194201));
#139334=CARTESIAN_POINT('Ctrl Pts',(17.4395563508728,17.0023769811862,6.43417218788605));
#139335=CARTESIAN_POINT('Ctrl Pts',(17.3644771451664,17.0463798735677,6.43848835062497));
#139336=CARTESIAN_POINT('Ctrl Pts',(17.2916709526714,17.0941996856768,6.4428045133639));
#139337=CARTESIAN_POINT('Ctrl Pts',(17.221535475533,17.1455579015066,6.44712067610282));
#139338=CARTESIAN_POINT('Ctrl Pts',(17.1536846541856,17.1952431288576,6.4512962402945));
#139339=CARTESIAN_POINT('Ctrl Pts',(17.0883335592487,17.2482394397186,6.45547180448618));
#139340=CARTESIAN_POINT('Ctrl Pts',(17.0258081406205,17.3042539310255,6.45964736867786));
#139341=CARTESIAN_POINT('Ctrl Pts',(16.9601247117373,17.3630975811267,6.46403383069041));
#139342=CARTESIAN_POINT('Ctrl Pts',(16.8975603248985,17.4252719095173,6.46842029270295));
#139343=CARTESIAN_POINT('Ctrl Pts',(16.8384470475511,17.4903957443787,6.4728067547155));
#139344=CARTESIAN_POINT('Ctrl Pts',(16.7793337702037,17.55551957924,6.47719321672805));
#139345=CARTESIAN_POINT('Ctrl Pts',(16.7236719107427,17.6235924232491,6.4815796787406));
#139346=CARTESIAN_POINT('Ctrl Pts',(16.6717415022697,17.6941974787273,6.48596614075315));
#139347=CARTESIAN_POINT('Ctrl Pts',(16.6219091295866,17.7619500256717,6.4901753857061));
#139348=CARTESIAN_POINT('Ctrl Pts',(16.5753265021954,17.8322867639503,6.49438463065906));
#139349=CARTESIAN_POINT('Ctrl Pts',(16.5322706261132,17.9048653345982,6.49859387561201));
#139350=CARTESIAN_POINT('Ctrl Pts',(16.4892771418592,17.9773387323843,6.50279702099131));
#139351=CARTESIAN_POINT('Ctrl Pts',(16.4498004872777,18.0520471246589,6.5070001663706));
#139352=CARTESIAN_POINT('Ctrl Pts',(16.4140760664827,18.128617007389,6.5112033117499));
#139353=CARTESIAN_POINT('Ctrl Pts',(16.3783931208862,18.2050979943158,6.51540157737789));
#139354=CARTESIAN_POINT('Ctrl Pts',(16.3464539443372,18.2834357700826,6.51959984300588));
#139355=CARTESIAN_POINT('Ctrl Pts',(16.3184487740251,18.3632310015746,6.52379810863387));
#139356=CARTESIAN_POINT('Ctrl Pts',(16.2904693914728,18.4429527559108,6.52799250840908));
#139357=CARTESIAN_POINT('Ctrl Pts',(16.2664169618498,18.5241288717768,6.53218690818429));
#139358=CARTESIAN_POINT('Ctrl Pts',(16.2464336691667,18.6063399717985,6.5363813079595));
#139359=CARTESIAN_POINT('Ctrl Pts',(16.2264610773219,18.6885070486605,6.54057346167876));
#139360=CARTESIAN_POINT('Ctrl Pts',(16.210553397436,18.7717075687093,6.54476561539801));
#139361=CARTESIAN_POINT('Ctrl Pts',(16.1988026788696,18.8555080269072,6.54895776911726));
#139362=CARTESIAN_POINT('Ctrl Pts',(16.1870533030452,18.9392989093172,6.55314944380363));
#139363=CARTESIAN_POINT('Ctrl Pts',(16.1794600117858,19.0236891460433,6.55734111849001));
#139364=CARTESIAN_POINT('Ctrl Pts',(16.1760633700115,19.1082371810286,6.56153279317638));
#139365=CARTESIAN_POINT('Ctrl Pts',(16.1746649834927,19.1430453357189,6.56325849219375));
#139366=CARTESIAN_POINT('Ctrl Pts',(16.173977295445,19.1778801783156,6.56498419121113));
#139367=CARTESIAN_POINT('Ctrl Pts',(16.1740005716256,19.2127107666517,6.5667098902285));
#139368=CARTESIAN_POINT('Ctrl Pts',(16.174000571626,19.2127107672549,6.56670989025838));
#139369=CARTESIAN_POINT('Ctrl Pts',(16.1740643617891,19.3081666398866,6.57143929947811));
#139370=CARTESIAN_POINT('Ctrl Pts',(16.1794711562484,19.4034153336876,6.57616870869783));
#139371=CARTESIAN_POINT('Ctrl Pts',(16.1901275024527,19.4979019278825,6.58089811791755));
#139372=CARTESIAN_POINT('Ctrl Pts',(16.200836414009,19.5928546031322,6.58565085624608));
#139373=CARTESIAN_POINT('Ctrl Pts',(16.2168466650982,19.6870374428256,6.59040359457461));
#139374=CARTESIAN_POINT('Ctrl Pts',(16.2380139506883,19.7799056526714,6.59515633290315));
#139375=CARTESIAN_POINT('Ctrl Pts',(16.2593038089226,19.8733116311407,6.59993659274364));
#139376=CARTESIAN_POINT('Ctrl Pts',(16.2858104835354,19.9653875176628,6.60471685258415));
#139377=CARTESIAN_POINT('Ctrl Pts',(16.3173390825683,20.0556005032904,6.60949711242465));
#139378=CARTESIAN_POINT('Ctrl Pts',(16.3253523527952,20.0785289255476,6.61071205742796));
#139379=CARTESIAN_POINT('Ctrl Pts',(16.3336897868424,20.101337126465,6.61192700243127));
#139380=CARTESIAN_POINT('Ctrl Pts',(16.3423477078173,20.1240166007785,6.61314194743458));
#139381=CARTESIAN_POINT('Ctrl Pts',(16.3721681801721,20.2021315014283,6.61732658182763));
#139382=CARTESIAN_POINT('Ctrl Pts',(16.405875193857,20.2789292632221,6.62151121622068));
#139383=CARTESIAN_POINT('Ctrl Pts',(16.4433319467771,20.3539960060928,6.62569585061373));
#139384=CARTESIAN_POINT('Ctrl Pts',(16.4807353846457,20.4289559007464,6.62987452869767));
#139385=CARTESIAN_POINT('Ctrl Pts',(16.5218777565726,20.5021892624269,6.63405320678161));
#139386=CARTESIAN_POINT('Ctrl Pts',(16.5665735905077,20.5733005393213,6.63823188486556));
#139387=CARTESIAN_POINT('Ctrl Pts',(16.6120705651436,20.6456864347473,6.64248546275099));
#139388=CARTESIAN_POINT('Ctrl Pts',(16.6612494744651,20.715872969927,6.64673904063643));
#139389=CARTESIAN_POINT('Ctrl Pts',(16.7138648542455,20.7834674854786,6.65099261852186));
#139390=CARTESIAN_POINT('Ctrl Pts',(16.7654601822184,20.8497515494465,6.65516373249982));
#139391=CARTESIAN_POINT('Ctrl Pts',(16.8203596287513,20.9135428198972,6.65933484647777));
#139392=CARTESIAN_POINT('Ctrl Pts',(16.8782881026494,20.9745003130227,6.66350596045572));
#139393=CARTESIAN_POINT('Ctrl Pts',(16.9361971380886,21.0354373512728,6.66767567477609));
#139394=CARTESIAN_POINT('Ctrl Pts',(16.9971328656301,21.0935421675084,6.67184538909647));
#139395=CARTESIAN_POINT('Ctrl Pts',(17.0607814536891,21.1485086312792,6.67601510341684));
#139396=CARTESIAN_POINT('Ctrl Pts',(17.1244277768583,21.2034731391074,6.68018466936089));
#139397=CARTESIAN_POINT('Ctrl Pts',(17.1907864198802,21.2552992164785,6.68435423530494));
#139398=CARTESIAN_POINT('Ctrl Pts',(17.2595094445545,21.3037201441908,6.68852380124899));
#139399=CARTESIAN_POINT('Ctrl Pts',(17.3306486859972,21.3538434919877,6.69283996398791));
#139400=CARTESIAN_POINT('Ctrl Pts',(17.4043212347442,21.4003174810233,6.69715612672683));
#139401=CARTESIAN_POINT('Ctrl Pts',(17.4801089073795,21.4428954114938,6.70147228946575));
#139402=CARTESIAN_POINT('Ctrl Pts',(17.5534278045502,21.4840863703576,6.70564785365743));
#139403=CARTESIAN_POINT('Ctrl Pts',(17.6287256988458,21.5216310329473,6.70982341784911));
#139404=CARTESIAN_POINT('Ctrl Pts',(17.7056010183996,21.555353969571,6.71399898204079));
#139405=CARTESIAN_POINT('Ctrl Pts',(17.7863591275902,21.5907801715548,6.71838544405333));
#139406=CARTESIAN_POINT('Ctrl Pts',(17.8688576552588,21.6219882241026,6.72277190606587));
#139407=CARTESIAN_POINT('Ctrl Pts',(17.9526121488768,21.6488336748263,6.72715836807841));
#139408=CARTESIAN_POINT('Ctrl Pts',(18.0363666424948,21.67567912555,6.73154483009094));
#139409=CARTESIAN_POINT('Ctrl Pts',(18.1213765216826,21.6981618996353,6.73593129210348));
#139410=CARTESIAN_POINT('Ctrl Pts',(18.20714644876,21.7161996598167,6.74031775411602));
#139411=CARTESIAN_POINT('Ctrl Pts',(18.288969974351,21.7334074759138,6.74450238850907));
#139412=CARTESIAN_POINT('Ctrl Pts',(18.3717897057139,21.7466343835296,6.74868702290212));
#139413=CARTESIAN_POINT('Ctrl Pts',(18.4551835868306,21.755771386146,6.75287165729516));
#139414=CARTESIAN_POINT('Ctrl Pts',(18.5384587670797,21.76489538337,6.75705033537911));
#139415=CARTESIAN_POINT('Ctrl Pts',(18.6223060204196,21.7699409891981,6.76122901346305));
#139416=CARTESIAN_POINT('Ctrl Pts',(18.7062923578697,21.7708500515787,6.765407691547));
#139417=CARTESIAN_POINT('Ctrl Pts',(18.7917840900588,21.7717754082492,6.76966126943243));
#139418=CARTESIAN_POINT('Ctrl Pts',(18.8774194697488,21.7684143685408,6.77391484731787));
#139419=CARTESIAN_POINT('Ctrl Pts',(18.9627354674093,21.7607607899466,6.77816842520331));
#139420=CARTESIAN_POINT('Ctrl Pts',(19.0463974479747,21.7532555909081,6.78233953918126));
#139421=CARTESIAN_POINT('Ctrl Pts',(19.1297518403942,21.7416228491976,6.78651065315921));
#139422=CARTESIAN_POINT('Ctrl Pts',(19.212363029601,21.7259093049076,6.79068176713716));
#139423=CARTESIAN_POINT('Ctrl Pts',(19.2949464978254,21.7102010334492,6.79485148145753));
#139424=CARTESIAN_POINT('Ctrl Pts',(19.3767868065737,21.6904147648581,6.79902119577791));
#139425=CARTESIAN_POINT('Ctrl Pts',(19.4574566774989,21.6666486792256,6.80319091009828));
#139426=CARTESIAN_POINT('Ctrl Pts',(19.5381236778438,21.6428834392924,6.80736047604233));
#139427=CARTESIAN_POINT('Ctrl Pts',(19.6176198821349,21.6151387947156,6.81153004198637));
#139428=CARTESIAN_POINT('Ctrl Pts',(19.6955326893839,21.5835629364142,6.81569960793041));
#139429=CARTESIAN_POINT('Ctrl Pts',(19.7761848148199,21.5508769098878,6.82001577066933));
#139430=CARTESIAN_POINT('Ctrl Pts',(19.8551396382569,21.5140854441414,6.82433193340825));
#139431=CARTESIAN_POINT('Ctrl Pts',(19.9319633694496,21.4734066313236,6.82864809614717));
#139432=CARTESIAN_POINT('Ctrl Pts',(20.0062845756792,21.4340529265547,6.83282366033885));
#139433=CARTESIAN_POINT('Ctrl Pts',(20.0786110173902,21.3910615273712,6.83699922453054));
#139434=CARTESIAN_POINT('Ctrl Pts',(20.148577822739,21.3446751353979,6.84117478872222));
#139435=CARTESIAN_POINT('Ctrl Pts',(20.2220784850956,21.2959458770392,6.84556125073476));
#139436=CARTESIAN_POINT('Ctrl Pts',(20.2929744068256,21.2434699978815,6.8499477127473));
#139437=CARTESIAN_POINT('Ctrl Pts',(20.3608819013654,21.1875766564972,6.85433417475984));
#139438=CARTESIAN_POINT('Ctrl Pts',(20.4287893959052,21.1316833151129,6.85872063677238));
#139439=CARTESIAN_POINT('Ctrl Pts',(20.4937080861994,21.0723729590138,6.86310709878492));
#139440=CARTESIAN_POINT('Ctrl Pts',(20.5553006227462,21.0100175211999,6.86749356079746));
#139441=CARTESIAN_POINT('Ctrl Pts',(20.6140591953844,20.9505311495128,6.87167819519051));
#139442=CARTESIAN_POINT('Ctrl Pts',(20.6700096812721,20.8880523361676,6.87586282958356));
#139443=CARTESIAN_POINT('Ctrl Pts',(20.7228319806689,20.8228769657355,6.8800474639766));
#139444=CARTESIAN_POINT('Ctrl Pts',(20.7755790940605,20.7577943643762,6.88422614206054));
#139445=CARTESIAN_POINT('Ctrl Pts',(20.8252065780214,20.6900231841701,6.88840482014449));
#139446=CARTESIAN_POINT('Ctrl Pts',(20.8714311671561,20.6198960237255,6.89258349822843));
#139447=CARTESIAN_POINT('Ctrl Pts',(20.9184842988301,20.5485118843294,6.89683707611387));
#139448=CARTESIAN_POINT('Ctrl Pts',(20.9620110031542,20.4746868150558,6.9010906539993));
#139449=CARTESIAN_POINT('Ctrl Pts',(21.0017554861493,20.3988068256412,6.90534423188474));
#139450=CARTESIAN_POINT('Ctrl Pts',(21.0407294447865,20.324397917889,6.90951534586269));
#139451=CARTESIAN_POINT('Ctrl Pts',(21.0760663016048,20.2480134825273,6.91368645984064));
#139452=CARTESIAN_POINT('Ctrl Pts',(21.1075695674518,20.1700451024153,6.91785757381859));
#139453=CARTESIAN_POINT('Ctrl Pts',(21.1390622620736,20.0921028853463,6.92202728813896));
#139454=CARTESIAN_POINT('Ctrl Pts',(21.1667237483346,20.0125782052865,6.92619700245933));
#139455=CARTESIAN_POINT('Ctrl Pts',(21.1904053024889,19.9318834787289,6.9303667167797));
#139456=CARTESIAN_POINT('Ctrl Pts',(21.214086013952,19.8511916236359,6.93453628272375));
#139457=CARTESIAN_POINT('Ctrl Pts',(21.2337869461661,19.7693302464837,6.93870584866779));
#139458=CARTESIAN_POINT('Ctrl Pts',(21.2494093711531,19.6867264923413,6.94287541461183));
#139459=CARTESIAN_POINT('Ctrl Pts',(21.2655810613302,19.601218492106,6.94719157735075));
#139460=CARTESIAN_POINT('Ctrl Pts',(21.2773820094429,19.5149154578639,6.95150774008968));
#139461=CARTESIAN_POINT('Ctrl Pts',(21.2847607940422,19.4283001877063,6.9558239028286));
#139462=CARTESIAN_POINT('Ctrl Pts',(21.2918992155093,19.3445064008638,6.95999946702028));
#139463=CARTESIAN_POINT('Ctrl Pts',(21.2948991834511,19.2604208803107,6.96417503121195));
#139464=CARTESIAN_POINT('Ctrl Pts',(21.2937672733171,19.1764817953117,6.96835059540363));
#139465=CARTESIAN_POINT('Ctrl Pts',(21.2925781930931,19.0883031466757,6.97273705741617));
#139466=CARTESIAN_POINT('Ctrl Pts',(21.2868289009944,19.0002866979193,6.97712351942872));
#139467=CARTESIAN_POINT('Ctrl Pts',(21.2765884850301,18.9129332360151,6.98150998144126));
#139468=CARTESIAN_POINT('Ctrl Pts',(21.2663480690658,18.8255797741109,6.9858964434538));
#139469=CARTESIAN_POINT('Ctrl Pts',(21.2516167014297,18.7388898583324,6.99028290546634));
#139470=CARTESIAN_POINT('Ctrl Pts',(21.2325245180282,18.6533484665025,6.99466936747888));
#139471=CARTESIAN_POINT('Ctrl Pts',(21.2143148178507,18.5717609882543,6.99885307745108));
#139472=CARTESIAN_POINT('Ctrl Pts',(21.1920707686424,18.4909145868902,7.00303678742329));
#139473=CARTESIAN_POINT('Ctrl Pts',(21.1658678428323,18.4112382886144,7.00722049739549));
#139474=CARTESIAN_POINT('Ctrl Pts',(21.1396995424231,18.3316672771986,7.01139867887684));
#139475=CARTESIAN_POINT('Ctrl Pts',(21.1095828937132,18.253263732009,7.01557686035819));
#139476=CARTESIAN_POINT('Ctrl Pts',(21.0756441741,18.1764457182422,7.01975504183954));
#139477=CARTESIAN_POINT('Ctrl Pts',(21.0417401170704,18.0997061609065,7.02392895602483));
#139478=CARTESIAN_POINT('Ctrl Pts',(21.0040219265333,18.0245493373816,7.02810287021013));
#139479=CARTESIAN_POINT('Ctrl Pts',(20.9626649803004,17.9513760856579,7.03227678439542));
#139480=CARTESIAN_POINT('Ctrl Pts',(20.9205833372596,17.8769206207443,7.03652383798201));
#139481=CARTESIAN_POINT('Ctrl Pts',(20.8747343543852,17.8045193682345,7.0407708915686));
#139482=CARTESIAN_POINT('Ctrl Pts',(20.8253528335361,17.7345707515561,7.04501794515519));
#139483=CARTESIAN_POINT('Ctrl Pts',(20.776870658013,17.66589605193,7.04918765062193));
#139484=CARTESIAN_POINT('Ctrl Pts',(20.7249838328577,17.5995857759597,7.05335735608868));
#139485=CARTESIAN_POINT('Ctrl Pts',(20.6699585805744,17.5359882465187,7.05752706155542));
#139486=CARTESIAN_POINT('Ctrl Pts',(20.6134022489947,17.4706211139121,7.06181278920193));
#139487=CARTESIAN_POINT('Ctrl Pts',(20.5535305417894,17.4081203454085,7.06609851684844));
#139488=CARTESIAN_POINT('Ctrl Pts',(20.4906759552872,17.3488266492843,7.07038424449495));
#139489=CARTESIAN_POINT('Ctrl Pts',(20.4278213687851,17.2895329531601,7.07466997214145));
#139490=CARTESIAN_POINT('Ctrl Pts',(20.3619843020148,17.2334466741789,7.07895569978796));
#139491=CARTESIAN_POINT('Ctrl Pts',(20.2935357313021,17.1808649545431,7.08324142743447));
#139492=CARTESIAN_POINT('Origin',(18.734,19.211,-1.76670989022852));
#139493=CARTESIAN_POINT('',(20.2909847804557,17.1841769303995,7.94987222326386));
#139494=CARTESIAN_POINT('',(20.2961055579379,17.1775279377506,7.883296963941));
#139495=CARTESIAN_POINT('',(20.2935357313021,17.1808649545432,-1.76670989022852));
#139496=CARTESIAN_POINT('',(16.1743644999821,19.2104398261047,7.43329008494582));
#139497=CARTESIAN_POINT('Ctrl Pts',(16.1781030359051,19.2104411453813,7.4332901097715));
#139498=CARTESIAN_POINT('Ctrl Pts',(16.1790025448085,19.6723916862602,7.4561794192865));
#139499=CARTESIAN_POINT('Ctrl Pts',(16.519742516428,20.9911304253782,7.52146066436197));
#139500=CARTESIAN_POINT('Ctrl Pts',(18.635203471302,22.2364801012593,7.62913384499793));
#139501=CARTESIAN_POINT('Ctrl Pts',(21.2244732853929,20.9317072417885,7.75630965167935));
#139502=CARTESIAN_POINT('Ctrl Pts',(21.4803857485738,18.507708892409,7.86322244443467));
#139503=CARTESIAN_POINT('Ctrl Pts',(20.6448527341026,17.4566900324871,7.9277433016295));
#139504=CARTESIAN_POINT('Ctrl Pts',(20.2909847804557,17.1841769303995,7.94987222326386));
#139505=CARTESIAN_POINT('Ctrl Pts',(20.2935357313021,17.1808649545431,7.14996298022642));
#139506=CARTESIAN_POINT('Ctrl Pts',(20.2269740491137,17.1297327296497,7.15413571681833));
#139507=CARTESIAN_POINT('Ctrl Pts',(20.1578294014536,17.0818270510226,7.15830845341025));
#139508=CARTESIAN_POINT('Ctrl Pts',(20.0864499301619,17.0374132898812,7.16248119000217));
#139509=CARTESIAN_POINT('Ctrl Pts',(20.0151086378096,16.9930232844536,7.16665169471068));
#139510=CARTESIAN_POINT('Ctrl Pts',(19.9415352849612,16.9521217307261,7.1708221994192));
#139511=CARTESIAN_POINT('Ctrl Pts',(19.8661074862141,16.914931046406,7.17499270412771));
#139512=CARTESIAN_POINT('Ctrl Pts',(19.7906974050045,16.8777490979546,7.17916222920968));
#139513=CARTESIAN_POINT('Ctrl Pts',(19.7134341556442,16.844276490702,7.18333175429165));
#139514=CARTESIAN_POINT('Ctrl Pts',(19.6347192600783,16.8146893326357,7.18750127937362));
#139515=CARTESIAN_POINT('Ctrl Pts',(19.5559992417777,16.7851002490487,7.19167107580666));
#139516=CARTESIAN_POINT('Ctrl Pts',(19.4758278207703,16.7593972773767,7.19584087223971));
#139517=CARTESIAN_POINT('Ctrl Pts',(19.3946244766586,16.737707599001,7.20001066867275));
#139518=CARTESIAN_POINT('Ctrl Pts',(19.3133366757596,16.7159953619416,7.20418480196672));
#139519=CARTESIAN_POINT('Ctrl Pts',(19.2310152538687,16.6983048726722,7.20835893526069));
#139520=CARTESIAN_POINT('Ctrl Pts',(19.1480922894468,16.6847126893758,7.21253306855467));
#139521=CARTESIAN_POINT('Ctrl Pts',(19.0651252830309,16.6711132870074,7.21670941881175));
#139522=CARTESIAN_POINT('Ctrl Pts',(18.9815565552246,16.6616165772755,7.22088576906883));
#139523=CARTESIAN_POINT('Ctrl Pts',(18.8978233253707,16.6562471904185,7.22506211932592));
#139524=CARTESIAN_POINT('Ctrl Pts',(18.8139434930286,16.6508684026883,7.2292457816542));
#139525=CARTESIAN_POINT('Ctrl Pts',(18.7298990438713,16.6496313793322,7.2334294439825));
#139526=CARTESIAN_POINT('Ctrl Pts',(18.6461270288959,16.6525085810288,7.23761310631078));
#139527=CARTESIAN_POINT('Ctrl Pts',(18.5794262634492,16.6547994600957,7.24094421252506));
#139528=CARTESIAN_POINT('Ctrl Pts',(18.5128982458229,16.6596975650841,7.24427531873934));
#139529=CARTESIAN_POINT('Ctrl Pts',(18.4467595506041,16.6671657042506,7.24760642495362));
#139530=CARTESIAN_POINT('Ctrl Pts',(18.3636741606704,16.6765474021004,7.25179105934667));
#139531=CARTESIAN_POINT('Ctrl Pts',(18.2808942658293,16.6900213769478,7.25597569373972));
#139532=CARTESIAN_POINT('Ctrl Pts',(18.1988547913486,16.7075584477249,7.26016032813276));
#139533=CARTESIAN_POINT('Ctrl Pts',(18.116932089905,16.7250705566525,7.26433900621672));
#139534=CARTESIAN_POINT('Ctrl Pts',(18.0357481614728,16.7466341786849,7.26851768430068));
#139535=CARTESIAN_POINT('Ctrl Pts',(17.9557323296054,16.77216842869,7.27269636238463));
#139536=CARTESIAN_POINT('Ctrl Pts',(17.8742822714585,16.7981603617751,7.27694994027007));
#139537=CARTESIAN_POINT('Ctrl Pts',(17.7940430771259,16.8282666158667,7.2812035181555));
#139538=CARTESIAN_POINT('Ctrl Pts',(17.7154562415191,16.8623474901426,7.28545709604093));
#139539=CARTESIAN_POINT('Ctrl Pts',(17.63839296507,16.8957676401673,7.28962821001889));
#139540=CARTESIAN_POINT('Ctrl Pts',(17.5629189921761,16.9330094826425,7.29379932399685));
#139541=CARTESIAN_POINT('Ctrl Pts',(17.4894331713713,16.9738917305867,7.2979704379748));
#139542=CARTESIAN_POINT('Ctrl Pts',(17.4159720094435,17.0147602600978,7.30214015229517));
#139543=CARTESIAN_POINT('Ctrl Pts',(17.3444980763215,17.059266545551,7.30630986661554));
#139544=CARTESIAN_POINT('Ctrl Pts',(17.2753861385062,17.1071830870871,7.31047958093591));
#139545=CARTESIAN_POINT('Ctrl Pts',(17.2062766599905,17.155097923547,7.31464914687994));
#139546=CARTESIAN_POINT('Ctrl Pts',(17.1395293872397,17.2064225119979,7.31881871282397));
#139547=CARTESIAN_POINT('Ctrl Pts',(17.0754894346056,17.2608864893358,7.322988278768));
#139548=CARTESIAN_POINT('Ctrl Pts',(17.0091979162384,17.3172653529285,7.32730444150692));
#139549=CARTESIAN_POINT('Ctrl Pts',(16.9458080406878,17.377008133023,7.33162060424584));
#139550=CARTESIAN_POINT('Ctrl Pts',(16.885663067504,17.4397714478444,7.33593676698476));
#139551=CARTESIAN_POINT('Ctrl Pts',(16.8274773104956,17.5004902542869,7.34011233117644));
#139552=CARTESIAN_POINT('Ctrl Pts',(16.7723285700598,17.5640354429535,7.34428789536812));
#139553=CARTESIAN_POINT('Ctrl Pts',(16.7204869451086,17.6300619310733,7.3484634595598));
#139554=CARTESIAN_POINT('Ctrl Pts',(16.6660269229228,17.6994232601449,7.35284992157234));
#139555=CARTESIAN_POINT('Ctrl Pts',(16.6152172172816,17.7715226597539,7.35723638358488));
#139556=CARTESIAN_POINT('Ctrl Pts',(16.5683186145658,17.845927058072,7.36162284559743));
#139557=CARTESIAN_POINT('Ctrl Pts',(16.52142001185,17.9203314563902,7.36600930760997));
#139558=CARTESIAN_POINT('Ctrl Pts',(16.4784327293519,17.9970403100744,7.37039576962251));
#139559=CARTESIAN_POINT('Ctrl Pts',(16.4395601204679,18.0755945044995,7.37478223163505));
#139560=CARTESIAN_POINT('Ctrl Pts',(16.399796394139,18.1559494788318,7.37926924910124));
#139561=CARTESIAN_POINT('Ctrl Pts',(16.3642056179145,18.2385006465143,7.38375626656742));
#139562=CARTESIAN_POINT('Ctrl Pts',(16.3330179090159,18.3228080169392,7.3882432840336));
#139563=CARTESIAN_POINT('Ctrl Pts',(16.3019356806123,18.4068302499339,7.39271512587964));
#139564=CARTESIAN_POINT('Ctrl Pts',(16.2752269677052,18.4925965155752,7.39718696772568));
#139565=CARTESIAN_POINT('Ctrl Pts',(16.2530742870064,18.5796462112197,7.40165880957171));
#139566=CARTESIAN_POINT('Ctrl Pts',(16.2309688572624,18.6665102326658,7.40612111312305));
#139567=CARTESIAN_POINT('Ctrl Pts',(16.2134002030055,18.7546518909164,7.41058341667439));
#139568=CARTESIAN_POINT('Ctrl Pts',(16.2005019648759,18.8435932689479,7.41504572022573));
#139569=CARTESIAN_POINT('Ctrl Pts',(16.1876417930138,18.9322721563783,7.41949485428535));
#139570=CARTESIAN_POINT('Ctrl Pts',(16.1794246278368,19.0217457093711,7.42394398834497));
#139571=CARTESIAN_POINT('Ctrl Pts',(16.1759333991831,19.1115250494595,7.42839312240459));
#139572=CARTESIAN_POINT('Ctrl Pts',(16.1746525201579,19.1444637323753,7.43002544244498));
#139573=CARTESIAN_POINT('Ctrl Pts',(16.1740072831437,19.177443453577,7.43165776248538));
#139574=CARTESIAN_POINT('Ctrl Pts',(16.1740000613162,19.2104396974995,7.43329008252577));
#139575=CARTESIAN_POINT('',(16.1738764730989,19.2121301833587,7.36670989022851));
#139576=CARTESIAN_POINT('Ctrl Pts',(20.2935357313021,17.1808649545431,7.08324142743447));
#139577=CARTESIAN_POINT('Ctrl Pts',(20.2268458566708,17.1296342530998,7.08741703894065));
#139578=CARTESIAN_POINT('Ctrl Pts',(20.1576774870271,17.0817303986562,7.09159265044683));
#139579=CARTESIAN_POINT('Ctrl Pts',(20.0864031281849,17.0373841694366,7.09576826195301));
#139580=CARTESIAN_POINT('Ctrl Pts',(20.0122177785098,16.9912267493648,7.10011441398756));
#139581=CARTESIAN_POINT('Ctrl Pts',(19.93575121291,16.948924058118,7.10446056602211));
#139582=CARTESIAN_POINT('Ctrl Pts',(19.8574497100952,16.910682467813,7.10880671805666));
#139583=CARTESIAN_POINT('Ctrl Pts',(19.7791482072804,16.872440877508,7.11315287009122));
#139584=CARTESIAN_POINT('Ctrl Pts',(19.6990123054848,16.8382605382041,7.11749902212576));
#139585=CARTESIAN_POINT('Ctrl Pts',(19.6175072439402,16.8082900820313,7.12184517416032));
#139586=CARTESIAN_POINT('Ctrl Pts',(19.5390311848803,16.7794334289094,7.12602980855336));
#139587=CARTESIAN_POINT('Ctrl Pts',(19.4589938470389,16.7543718340009,7.13021444294641));
#139588=CARTESIAN_POINT('Ctrl Pts',(19.3777970941006,16.733274167381,7.13439907733946));
#139589=CARTESIAN_POINT('Ctrl Pts',(19.2967159146901,16.7122065306782,7.1385777554234));
#139590=CARTESIAN_POINT('Ctrl Pts',(19.2144790396056,16.6950917298573,7.14275643350734));
#139591=CARTESIAN_POINT('Ctrl Pts',(19.1315065014626,16.6820499053372,7.14693511159128));
#139592=CARTESIAN_POINT('Ctrl Pts',(19.0470467402047,16.6687743154856,7.15118868947672));
#139593=CARTESIAN_POINT('Ctrl Pts',(18.9618251354749,16.6597193207395,7.15544226736216));
#139594=CARTESIAN_POINT('Ctrl Pts',(18.8762989641012,16.654957941501,7.15969584524759));
#139595=CARTESIAN_POINT('Ctrl Pts',(18.7924308844501,16.6502888708901,7.16386695922554));
#139596=CARTESIAN_POINT('Ctrl Pts',(18.7082704224839,16.6497484479464,7.1680380732035));
#139597=CARTESIAN_POINT('Ctrl Pts',(18.6242553740812,16.6533534026215,7.17220918718145));
#139598=CARTESIAN_POINT('Ctrl Pts',(18.5402685177394,16.6569571476192,7.17637890150182));
#139599=CARTESIAN_POINT('Ctrl Pts',(18.4564274372811,16.6647034879404,7.1805486158222));
#139600=CARTESIAN_POINT('Ctrl Pts',(18.3731691163825,16.6765570486934,7.18471833014257));
#139601=CARTESIAN_POINT('Ctrl Pts',(18.2899137581723,16.6884101876458,7.18888789608661));
#139602=CARTESIAN_POINT('Ctrl Pts',(18.2072415736113,16.7043701907562,7.19305746203066));
#139603=CARTESIAN_POINT('Ctrl Pts',(18.1255822535274,16.7243500757491,7.1972270279747));
#139604=CARTESIAN_POINT('Ctrl Pts',(18.041051892487,16.7450324288504,7.20154319071362));
#139605=CARTESIAN_POINT('Ctrl Pts',(17.9576074580676,16.7700224760727,7.20585935345254));
#139606=CARTESIAN_POINT('Ctrl Pts',(17.8757097136975,16.799167131736,7.21017551619146));
#139607=CARTESIAN_POINT('Ctrl Pts',(17.7964797797362,16.8273624033065,7.21435108038314));
#139608=CARTESIAN_POINT('Ctrl Pts',(17.7186977338734,16.8594455439839,7.21852664457482));
#139609=CARTESIAN_POINT('Ctrl Pts',(17.6427597031134,16.8952291532946,7.2227022087665));
#139610=CARTESIAN_POINT('Ctrl Pts',(17.5629862229451,16.9328201076441,7.22708867077904));
#139611=CARTESIAN_POINT('Ctrl Pts',(17.485248450476,16.9744949002993,7.23147513279158));
#139612=CARTESIAN_POINT('Ctrl Pts',(17.409973629261,17.0199833023028,7.23586159480412));
#139613=CARTESIAN_POINT('Ctrl Pts',(17.3346988080461,17.0654717043064,7.24024805681667));
#139614=CARTESIAN_POINT('Ctrl Pts',(17.2618873758783,17.1147733273606,7.24463451882921));
#139615=CARTESIAN_POINT('Ctrl Pts',(17.1919269101811,17.1675689183003,7.24902098084175));
#139616=CARTESIAN_POINT('Ctrl Pts',(17.1258771580207,17.2174132934338,7.25316224442401));
#139617=CARTESIAN_POINT('Ctrl Pts',(17.0621112325389,17.2705657001619,7.25730350800627));
#139618=CARTESIAN_POINT('Ctrl Pts',(17.0009846311416,17.326787238314,7.26144477158852));
#139619=CARTESIAN_POINT('Ctrl Pts',(16.9399453026366,17.3829285067285,7.26558012252321));
#139620=CARTESIAN_POINT('Ctrl Pts',(16.8815381604268,17.4421298917806,7.2697154734579));
#139621=CARTESIAN_POINT('Ctrl Pts',(16.8260879518441,17.5041105435613,7.27385082439259));
#139622=CARTESIAN_POINT('Ctrl Pts',(16.7707013118209,17.5660201402305,7.27798143452813));
#139623=CARTESIAN_POINT('Ctrl Pts',(16.7182651826551,17.6307023247235,7.28211204466367));
#139624=CARTESIAN_POINT('Ctrl Pts',(16.6690684130045,17.6978385608177,7.28624265479921));
#139625=CARTESIAN_POINT('Ctrl Pts',(16.6199019406792,17.7649334517505,7.29037072114092));
#139626=CARTESIAN_POINT('Ctrl Pts',(16.5739711466916,17.8344790168686,7.29449878748264));
#139627=CARTESIAN_POINT('Ctrl Pts',(16.5315246255303,17.9061236744984,7.29862685382436));
#139628=CARTESIAN_POINT('Ctrl Pts',(16.4890908665707,17.977746791056,7.3027536789992));
#139629=CARTESIAN_POINT('Ctrl Pts',(16.4501395400176,18.0514673424197,7.30688050417405));
#139630=CARTESIAN_POINT('Ctrl Pts',(16.4148750854129,18.1269060785424,7.3110073293489));
#139631=CARTESIAN_POINT('Ctrl Pts',(16.3796101195078,18.2023459084537,7.31513421435872));
#139632=CARTESIAN_POINT('Ctrl Pts',(16.3480323287909,18.2795035453344,7.31926109936854));
#139633=CARTESIAN_POINT('Ctrl Pts',(16.3202988339461,18.3579779129531,7.32338798437835));
#139634=CARTESIAN_POINT('Ctrl Pts',(16.2925397363851,18.4365247257132,7.32751867920247));
#139635=CARTESIAN_POINT('Ctrl Pts',(16.2686321752694,18.516390251046,7.33164937402659));
#139636=CARTESIAN_POINT('Ctrl Pts',(16.2486837569799,18.5971570459957,7.33578006885071));
#139637=CARTESIAN_POINT('Ctrl Pts',(16.2287250388403,18.6779655427923,7.33991289645232));
#139638=CARTESIAN_POINT('Ctrl Pts',(16.2127296214478,18.7596757735077,7.34404572405394));
#139639=CARTESIAN_POINT('Ctrl Pts',(16.2007537416511,18.8418612800569,7.34817855165556));
#139640=CARTESIAN_POINT('Ctrl Pts',(16.1887593096482,18.9241741027186,7.35231778154836));
#139641=CARTESIAN_POINT('Ctrl Pts',(16.180796886798,19.0069632027562,7.35645701144116));
#139642=CARTESIAN_POINT('Ctrl Pts',(16.176870697397,19.0897988045885,7.36059624133397));
#139643=CARTESIAN_POINT('Ctrl Pts',(16.1749377014765,19.1305815748691,7.36263412429881));
#139644=CARTESIAN_POINT('Ctrl Pts',(16.1739822581149,19.1713756409971,7.36467200726366));
#139645=CARTESIAN_POINT('Ctrl Pts',(16.1740002494514,19.2121301287168,7.36670989022851));
#139646=CARTESIAN_POINT('Ctrl Pts',(16.1703788196327,19.2121317274208,7.36670989022851));
#139647=CARTESIAN_POINT('Ctrl Pts',(16.1700290407744,19.2754624167648,7.36987218932674));
#139648=CARTESIAN_POINT('Ctrl Pts',(16.2008981366677,20.1874206696652,7.41542642398544));
#139649=CARTESIAN_POINT('Ctrl Pts',(17.2895132664939,21.8712161675055,7.50337259420461));
#139650=CARTESIAN_POINT('Ctrl Pts',(20.1889475365473,21.8655093043776,7.63054840088606));
#139651=CARTESIAN_POINT('Ctrl Pts',(21.7469837784997,19.4347114040786,7.75718985746491));
#139652=CARTESIAN_POINT('Ctrl Pts',(20.9598514275375,17.6886843310748,7.84143937848329));
#139653=CARTESIAN_POINT('Ctrl Pts',(20.2961055579348,17.1775279377483,7.88329696394119));
#139654=CARTESIAN_POINT('Origin',(18.734,19.211,-1.76670989022852));
#139655=CARTESIAN_POINT('',(20.2935357313021,17.1808649545431,8.74981199697632));
#139656=CARTESIAN_POINT('',(20.2935357313021,17.1808649545431,8.68337763228924));
#139657=CARTESIAN_POINT('',(20.2935357313021,17.1808649545432,-1.76670989022852));
#139658=CARTESIAN_POINT('',(16.1740010826189,19.2133543592346,8.23329012251325));
#139659=CARTESIAN_POINT('Ctrl Pts',(16.1740010826189,19.2133543592346,8.23329012251325));
#139660=CARTESIAN_POINT('Ctrl Pts',(16.1741014808466,19.322521792358,8.23871812867197));
#139661=CARTESIAN_POINT('Ctrl Pts',(16.1811885397039,19.4313771444072,8.24414613483068));
#139662=CARTESIAN_POINT('Ctrl Pts',(16.1951208364047,19.5391654958424,8.2495741409894));
#139663=CARTESIAN_POINT('Ctrl Pts',(16.2083299266963,19.6413587018203,8.25472038679463));
#139664=CARTESIAN_POINT('Ctrl Pts',(16.2276915596972,19.7425933354954,8.25986663259986));
#139665=CARTESIAN_POINT('Ctrl Pts',(16.253046772176,19.84224565848,8.2650128784051));
#139666=CARTESIAN_POINT('Ctrl Pts',(16.2736641888712,19.9232772597465,8.26919751279815));
#139667=CARTESIAN_POINT('Ctrl Pts',(16.2982940662942,20.0034485022604,8.27338214719119));
#139668=CARTESIAN_POINT('Ctrl Pts',(16.3268482220627,20.0823324956487,8.27756678158424));
#139669=CARTESIAN_POINT('Ctrl Pts',(16.3553617345248,20.1611042074362,8.28174545966818));
#139670=CARTESIAN_POINT('Ctrl Pts',(16.3877882750863,20.2385918806366,8.28592413775213));
#139671=CARTESIAN_POINT('Ctrl Pts',(16.42398920314,20.3143812207891,8.29010281583607));
#139672=CARTESIAN_POINT('Ctrl Pts',(16.4608390068118,20.391529030395,8.29435639372151));
#139673=CARTESIAN_POINT('Ctrl Pts',(16.5015997218018,20.466916555597,8.29860997160694));
#139674=CARTESIAN_POINT('Ctrl Pts',(16.5460727818106,20.5401254598065,8.30286354949237));
#139675=CARTESIAN_POINT('Ctrl Pts',(16.5896836447691,20.6119150665525,8.30703466347033));
#139676=CARTESIAN_POINT('Ctrl Pts',(16.6368639453123,20.6816093608383,8.31120577744828));
#139677=CARTESIAN_POINT('Ctrl Pts',(16.6873797310323,20.7488379221006,8.31537689142623));
#139678=CARTESIAN_POINT('Ctrl Pts',(16.7378785656926,20.8160439241699,8.3195466057466));
#139679=CARTESIAN_POINT('Ctrl Pts',(16.791710386553,20.8807854689741,8.32371632006698));
#139680=CARTESIAN_POINT('Ctrl Pts',(16.8485987415146,20.9427222913913,8.32788603438735));
#139681=CARTESIAN_POINT('Ctrl Pts',(16.9054850721444,21.0046569098306,8.33205560033139));
#139682=CARTESIAN_POINT('Ctrl Pts',(16.9654274088047,21.0637866660881,8.33622516627544));
#139683=CARTESIAN_POINT('Ctrl Pts',(17.0281108772061,21.1198065121257,8.34039473221948));
#139684=CARTESIAN_POINT('Ctrl Pts',(17.0929982190279,21.177795946842,8.3447108949584));
#139685=CARTESIAN_POINT('Ctrl Pts',(17.1608226421282,21.2324523620818,8.34902705769732));
#139686=CARTESIAN_POINT('Ctrl Pts',(17.2311971876104,21.283482498617,8.35334322043624));
#139687=CARTESIAN_POINT('Ctrl Pts',(17.2992792896757,21.3328503338221,8.35751878462792));
#139688=CARTESIAN_POINT('Ctrl Pts',(17.3697475047297,21.3788242964687,8.3616943488196));
#139689=CARTESIAN_POINT('Ctrl Pts',(17.4422231594137,21.4211838371785,8.36586991301128));
#139690=CARTESIAN_POINT('Ctrl Pts',(17.5183593871213,21.4656828575893,8.37025637502382));
#139691=CARTESIAN_POINT('Ctrl Pts',(17.5967106568094,21.506192463235,8.37464283703637));
#139692=CARTESIAN_POINT('Ctrl Pts',(17.6768123961766,21.5425133219268,8.3790292990489));
#139693=CARTESIAN_POINT('Ctrl Pts',(17.7569141355439,21.5788341806186,8.38341576106144));
#139694=CARTESIAN_POINT('Ctrl Pts',(17.8387657767032,21.6109661511407,8.38780222307398));
#139695=CARTESIAN_POINT('Ctrl Pts',(17.921884774769,21.638770347654,8.39218868508652));
#139696=CARTESIAN_POINT('Ctrl Pts',(18.001179344522,21.66529523187,8.39637331947957));
#139697=CARTESIAN_POINT('Ctrl Pts',(18.0819223576084,21.6879805757247,8.40055795387261));
#139698=CARTESIAN_POINT('Ctrl Pts',(18.1637071353304,21.7066694589843,8.40474258826566));
#139699=CARTESIAN_POINT('Ctrl Pts',(18.2453755025443,21.7253317409318,8.4089212663496));
#139700=CARTESIAN_POINT('Ctrl Pts',(18.3280822444037,21.7400087597643,8.41309994443355));
#139701=CARTESIAN_POINT('Ctrl Pts',(18.4114039612994,21.7505928405582,8.4172786225175));
#139702=CARTESIAN_POINT('Ctrl Pts',(18.4962191600882,21.7613666333938,8.42153220040293));
#139703=CARTESIAN_POINT('Ctrl Pts',(18.5816711403845,21.7678991601646,8.42578577828837));
#139704=CARTESIAN_POINT('Ctrl Pts',(18.6673006671489,21.7701309460434,8.43003935617381));
#139705=CARTESIAN_POINT('Ctrl Pts',(18.7512700984447,21.7723194643981,8.43421047015176));
#139706=CARTESIAN_POINT('Ctrl Pts',(18.8354097724167,21.7703724977257,8.43838158412971));
#139707=CARTESIAN_POINT('Ctrl Pts',(18.9192815899904,21.7642862613523,8.44255269810766));
#139708=CARTESIAN_POINT('Ctrl Pts',(19.0031252635657,21.7582020672744,8.44672241242803));
#139709=CARTESIAN_POINT('Ctrl Pts',(19.0867008008049,21.7479813952832,8.45089212674841));
#139710=CARTESIAN_POINT('Ctrl Pts',(19.1695724543108,21.7336725187875,8.45506184106878));
#139711=CARTESIAN_POINT('Ctrl Pts',(19.2524411588877,21.719364151463,8.45923140701282));
#139712=CARTESIAN_POINT('Ctrl Pts',(19.3346055763514,21.7009679479898,8.46340097295687));
#139713=CARTESIAN_POINT('Ctrl Pts',(19.4156387740957,21.678583551098,8.46757053890091));
#139714=CARTESIAN_POINT('Ctrl Pts',(19.4995209991075,21.6554121464256,8.47188670163983));
#139715=CARTESIAN_POINT('Ctrl Pts',(19.5821904685913,21.6279670209743,8.47620286437875));
#139716=CARTESIAN_POINT('Ctrl Pts',(19.6631911444339,21.5964148102805,8.48051902711767));
#139717=CARTESIAN_POINT('Ctrl Pts',(19.7415532317807,21.5658904095313,8.48469459130935));
#139718=CARTESIAN_POINT('Ctrl Pts',(19.8183531671025,21.5315226265231,8.48887015550103));
#139719=CARTESIAN_POINT('Ctrl Pts',(19.8932005345677,21.4935104864289,8.49304571969271));
#139720=CARTESIAN_POINT('Ctrl Pts',(19.9718282646309,21.4535784435038,8.49743218170526));
#139721=CARTESIAN_POINT('Ctrl Pts',(20.0483004884277,21.409624506264,8.5018186437178));
#139722=CARTESIAN_POINT('Ctrl Pts',(20.1221981349569,21.3619314117615,8.50620510573034));
#139723=CARTESIAN_POINT('Ctrl Pts',(20.196095781486,21.314238317259,8.51059156774288));
#139724=CARTESIAN_POINT('Ctrl Pts',(20.267418424621,21.2628064665597,8.51497802975542));
#139725=CARTESIAN_POINT('Ctrl Pts',(20.3357880909557,21.2079664272773,8.51936449176796));
#139726=CARTESIAN_POINT('Ctrl Pts',(20.4010119675942,21.1556496594946,8.52354912616101));
#139727=CARTESIAN_POINT('Ctrl Pts',(20.463791413314,21.1000367097147,8.52773376055406));
#139728=CARTESIAN_POINT('Ctrl Pts',(20.5237743555653,21.0413845924179,8.53191839494711));
#139729=CARTESIAN_POINT('Ctrl Pts',(20.5836719195227,20.9828159591504,8.53609707303105));
#139730=CARTESIAN_POINT('Ctrl Pts',(20.6407805603833,20.9212170697946,8.540275751115));
#139731=CARTESIAN_POINT('Ctrl Pts',(20.6947805623983,20.8568856540237,8.54445442919894));
#139732=CARTESIAN_POINT('Ctrl Pts',(20.7497484756402,20.7914011438593,8.54870800708438));
#139733=CARTESIAN_POINT('Ctrl Pts',(20.8014948330691,20.723085484341,8.55296158496981));
#139734=CARTESIAN_POINT('Ctrl Pts',(20.8497210505506,20.6522926268656,8.55721516285525));
#139735=CARTESIAN_POINT('Ctrl Pts',(20.8970123087005,20.5828722270733,8.5613862768332));
#139736=CARTESIAN_POINT('Ctrl Pts',(20.940918427529,20.5110702205224,8.56555739081115));
#139737=CARTESIAN_POINT('Ctrl Pts',(20.9811990900047,20.4372529306315,8.56972850478911));
#139738=CARTESIAN_POINT('Ctrl Pts',(21.021466235915,20.3634604108451,8.57389821910948));
#139739=CARTESIAN_POINT('Ctrl Pts',(21.058110121399,20.2876543542439,8.57806793342985));
#139740=CARTESIAN_POINT('Ctrl Pts',(21.0909354749524,20.2102272849111,8.58223764775022));
#139741=CARTESIAN_POINT('Ctrl Pts',(21.1237596604389,20.1328029707657,8.58640721369427));
#139742=CARTESIAN_POINT('Ctrl Pts',(21.1527654053819,20.0537581824513,8.59057677963831));
#139743=CARTESIAN_POINT('Ctrl Pts',(21.1778054030264,19.9735058374459,8.59474634558236));
#139744=CARTESIAN_POINT('Ctrl Pts',(21.2037257760978,19.8904319189922,8.59906250832128));
#139745=CARTESIAN_POINT('Ctrl Pts',(21.2253961847597,19.8060644520148,8.6033786710602));
#139746=CARTESIAN_POINT('Ctrl Pts',(21.242709898346,19.7208770890524,8.60769483379912));
#139747=CARTESIAN_POINT('Ctrl Pts',(21.2594596195334,19.6384646954784,8.6118703979908));
#139748=CARTESIAN_POINT('Ctrl Pts',(21.2721321012068,19.5552854746202,8.61604596218248));
#139749=CARTESIAN_POINT('Ctrl Pts',(21.2806833673555,19.4717754329589,8.62022152637416));
#139750=CARTESIAN_POINT('Ctrl Pts',(21.2896665376286,19.3840474976196,8.6246079883867));
#139751=CARTESIAN_POINT('Ctrl Pts',(21.2941011966021,19.2959550268227,8.62899445039924));
#139752=CARTESIAN_POINT('Ctrl Pts',(21.2939982462078,19.2080034331647,8.63338091241178));
#139753=CARTESIAN_POINT('Ctrl Pts',(21.2938952958136,19.1200518395066,8.63776737442432));
#139754=CARTESIAN_POINT('Ctrl Pts',(21.2892548426303,19.0322416983818,8.64215383643686));
#139755=CARTESIAN_POINT('Ctrl Pts',(21.2801502518719,18.9450697555886,8.6465402984494));
#139756=CARTESIAN_POINT('Ctrl Pts',(21.2712189218945,18.8595566988775,8.65084328588802));
#139757=CARTESIAN_POINT('Ctrl Pts',(21.2579577430371,18.7743304226481,8.65514627332665));
#139758=CARTESIAN_POINT('Ctrl Pts',(21.2403952839669,18.6898640479603,8.65944926076527));
#139759=CARTESIAN_POINT('Ctrl Pts',(21.2233438126719,18.607855261057,8.66362705081729));
#139760=CARTESIAN_POINT('Ctrl Pts',(21.2022379877299,18.5265632615501,8.66780484086931));
#139761=CARTESIAN_POINT('Ctrl Pts',(21.1771565043192,18.4464175679479,8.67198263092133));
#139762=CARTESIAN_POINT('Ctrl Pts',(21.1520996593001,18.3663506041782,8.67615631698851));
#139763=CARTESIAN_POINT('Ctrl Pts',(21.1230750469804,18.2874281469208,8.6803300030557));
#139764=CARTESIAN_POINT('Ctrl Pts',(21.0902120820861,18.2100681220825,8.68450368912288));
#139765=CARTESIAN_POINT('Ctrl Pts',(21.0573715401327,18.1327608812602,8.68867452741549));
#139766=CARTESIAN_POINT('Ctrl Pts',(21.0206980272887,18.0570143773557,8.6928453657081));
#139767=CARTESIAN_POINT('Ctrl Pts',(20.9803698805643,17.9832287022033,8.69701620400071));
#139768=CARTESIAN_POINT('Ctrl Pts',(20.940057152362,17.909471237275,8.70118544767101));
#139769=CARTESIAN_POINT('Ctrl Pts',(20.8960927884101,17.8376735138885,8.70535469134131));
#139770=CARTESIAN_POINT('Ctrl Pts',(20.8487014663918,17.7682118284237,8.70952393501162));
#139771=CARTESIAN_POINT('Ctrl Pts',(20.8012991468732,17.6987340238706,8.71369414618519));
#139772=CARTESIAN_POINT('Ctrl Pts',(20.7504685354779,17.631593723403,8.71786435735875));
#139773=CARTESIAN_POINT('Ctrl Pts',(20.6964775867251,17.5671381683361,8.72203456853232));
#139774=CARTESIAN_POINT('Ctrl Pts',(20.6424782965623,17.5026726551144,8.72620542398872));
#139775=CARTESIAN_POINT('Ctrl Pts',(20.58531800187,17.4408930576723,8.73037627944512));
#139776=CARTESIAN_POINT('Ctrl Pts',(20.5253036550083,17.3821120276097,8.73454713490153));
#139777=CARTESIAN_POINT('Ctrl Pts',(20.4652395196375,17.32328223221,8.73872145054181));
#139778=CARTESIAN_POINT('Ctrl Pts',(20.4023169461193,17.2674562791756,8.74289576618209));
#139779=CARTESIAN_POINT('Ctrl Pts',(20.3368776257449,17.2149079888727,8.74707008182237));
#139780=CARTESIAN_POINT('Ctrl Pts',(20.3225496033287,17.2034024738844,8.74798405354036));
#139781=CARTESIAN_POINT('Ctrl Pts',(20.3081010462363,17.1920539289557,8.74889802525834));
#139782=CARTESIAN_POINT('Ctrl Pts',(20.2935357313021,17.1808649545431,8.74981199697633));
#139783=CARTESIAN_POINT('Ctrl Pts',(20.2909847804557,17.1841769303995,7.94987222326386));
#139784=CARTESIAN_POINT('Ctrl Pts',(19.9669549252628,16.9346420965791,7.97013523718998));
#139785=CARTESIAN_POINT('Ctrl Pts',(18.7905372649548,16.3911014087415,8.03279018667658));
#139786=CARTESIAN_POINT('Ctrl Pts',(16.7471750875427,17.0720885005601,8.12726281551246));
#139787=CARTESIAN_POINT('Ctrl Pts',(16.180230297531,18.573538664413,8.20147243042223));
#139788=CARTESIAN_POINT('Ctrl Pts',(16.1744184457826,19.2133537191784,8.23329010977151));
#139789=CARTESIAN_POINT('',(16.1740010575059,19.2086731074563,8.16670989022852));
#139790=CARTESIAN_POINT('Ctrl Pts',(20.2961055579348,17.1775279377483,7.88329696394119));
#139791=CARTESIAN_POINT('Ctrl Pts',(20.2876322389503,17.1710025620435,7.88383131404377));
#139792=CARTESIAN_POINT('Ctrl Pts',(19.6033699010056,16.6514603046632,7.92675759970683));
#139793=CARTESIAN_POINT('Ctrl Pts',(17.6781136453352,16.37403049238,8.01207582093036));
#139794=CARTESIAN_POINT('Ctrl Pts',(16.2739021846612,17.9910560858828,8.10601244625689));
#139795=CARTESIAN_POINT('Ctrl Pts',(16.1718447049445,19.0247813383249,8.15755713602294));
#139796=CARTESIAN_POINT('Ctrl Pts',(16.1735502234357,19.2086726976739,8.16670989022852));
#139797=CARTESIAN_POINT('Ctrl Pts',(16.1740010575059,19.2086731074563,8.16670989022852));
#139798=CARTESIAN_POINT('Ctrl Pts',(16.1739251952239,19.2921352174732,8.17086478789788));
#139799=CARTESIAN_POINT('Ctrl Pts',(16.1779353066412,19.375721983002,8.17501968556725));
#139800=CARTESIAN_POINT('Ctrl Pts',(16.1860403077383,19.458994771335,8.17917458323661));
#139801=CARTESIAN_POINT('Ctrl Pts',(16.1940671586084,19.5414646248839,8.18328941845664));
#139802=CARTESIAN_POINT('Ctrl Pts',(16.206110236511,19.6236260477268,8.18740425367667));
#139803=CARTESIAN_POINT('Ctrl Pts',(16.2221259449782,19.7050533692914,8.1915190888967));
#139804=CARTESIAN_POINT('Ctrl Pts',(16.238134689091,19.7864452825742,8.19563213480029));
#139805=CARTESIAN_POINT('Ctrl Pts',(16.2581125446655,19.8671032636359,8.19974518070388));
#139806=CARTESIAN_POINT('Ctrl Pts',(16.2819644394347,19.9466096857188,8.20385822660747));
#139807=CARTESIAN_POINT('Ctrl Pts',(16.3058135810413,20.0261069305807,8.20797079775279));
#139808=CARTESIAN_POINT('Ctrl Pts',(16.3335357367831,20.1044524267965,8.21208336889812));
#139809=CARTESIAN_POINT('Ctrl Pts',(16.364985800536,20.1812431255815,8.21619594004344));
#139810=CARTESIAN_POINT('Ctrl Pts',(16.3969970744394,20.2594041147404,8.22038189789759));
#139811=CARTESIAN_POINT('Ctrl Pts',(16.4328704281986,20.3359537977656,8.22456785575174));
#139812=CARTESIAN_POINT('Ctrl Pts',(16.4724022025115,20.4104896424709,8.22875381360589));
#139813=CARTESIAN_POINT('Ctrl Pts',(16.5112918107484,20.4838147044136,8.23287177349698));
#139814=CARTESIAN_POINT('Ctrl Pts',(16.5537215594669,20.555190490736,8.23698973338807));
#139815=CARTESIAN_POINT('Ctrl Pts',(16.5994527799559,20.6242615346786,8.24110769327916));
#139816=CARTESIAN_POINT('Ctrl Pts',(16.6463167081171,20.6950433858238,8.24532765011484));
#139817=CARTESIAN_POINT('Ctrl Pts',(16.696647513794,20.7634043768934,8.24954760695052));
#139818=CARTESIAN_POINT('Ctrl Pts',(16.7501447185242,20.828998214511,8.2537675637862));
#139819=CARTESIAN_POINT('Ctrl Pts',(16.8036419232544,20.8945920521286,8.25798752062187));
#139820=CARTESIAN_POINT('Ctrl Pts',(16.8603051182411,20.9574183953713,8.26220747745755));
#139821=CARTESIAN_POINT('Ctrl Pts',(16.9197953580223,21.0171731691692,8.26642743429323));
#139822=CARTESIAN_POINT('Ctrl Pts',(16.9787876447051,21.0764277756308,8.27061206868628));
#139823=CARTESIAN_POINT('Ctrl Pts',(17.040795780927,21.1328994502153,8.27479670307933));
#139824=CARTESIAN_POINT('Ctrl Pts',(17.1055265727616,21.1862656268913,8.27898133747238));
#139825=CARTESIAN_POINT('Ctrl Pts',(17.170165228326,21.2395558434202,8.28316001555633));
#139826=CARTESIAN_POINT('Ctrl Pts',(17.2375184898922,21.2897490519969,8.28733869364028));
#139827=CARTESIAN_POINT('Ctrl Pts',(17.3072561423607,21.3365592122283,8.29151737172423));
#139828=CARTESIAN_POINT('Ctrl Pts',(17.3782437921302,21.3842084109399,8.29577094960966));
#139829=CARTESIAN_POINT('Ctrl Pts',(17.4517018138305,21.4283517444168,8.30002452749509));
#139830=CARTESIAN_POINT('Ctrl Pts',(17.5272463530815,21.4687301954948,8.30427810538053));
#139831=CARTESIAN_POINT('Ctrl Pts',(17.6013263140261,21.5083258315065,8.30844921935848));
#139832=CARTESIAN_POINT('Ctrl Pts',(17.6774121876527,21.5443010347693,8.31262033333643));
#139833=CARTESIAN_POINT('Ctrl Pts',(17.7551140500804,21.5764560442016,8.31679144731439));
#139834=CARTESIAN_POINT('Ctrl Pts',(17.8327898388977,21.60860026371,8.32096116163476));
#139835=CARTESIAN_POINT('Ctrl Pts',(17.9120801148581,21.6369266595076,8.32513087595513));
#139836=CARTESIAN_POINT('Ctrl Pts',(17.9925737212263,21.6612830598002,8.3293005902755));
#139837=CARTESIAN_POINT('Ctrl Pts',(18.0730644632865,21.6856385933875,8.33347015621954));
#139838=CARTESIAN_POINT('Ctrl Pts',(18.1547580100544,21.7060242799309,8.33763972216358));
#139839=CARTESIAN_POINT('Ctrl Pts',(18.2372280581079,21.7223378183249,8.34180928810762));
#139840=CARTESIAN_POINT('Ctrl Pts',(18.3225976513133,21.7392249206039,8.34612545084654));
#139841=CARTESIAN_POINT('Ctrl Pts',(18.4087988479274,21.7517480910506,8.35044161358546));
#139842=CARTESIAN_POINT('Ctrl Pts',(18.4953492973483,21.7598518674344,8.35475777632438));
#139843=CARTESIAN_POINT('Ctrl Pts',(18.5790803749828,21.7676916641549,8.35893334051606));
#139844=CARTESIAN_POINT('Ctrl Pts',(18.663137828366,21.7713955951849,8.36310890470775));
#139845=CARTESIAN_POINT('Ctrl Pts',(18.7470834485358,21.770966566847,8.36728446889943));
#139846=CARTESIAN_POINT('Ctrl Pts',(18.8352689624187,21.7705158693076,8.37167093091197));
#139847=CARTESIAN_POINT('Ctrl Pts',(18.923330465857,21.7655037616187,8.37605739292451));
#139848=CARTESIAN_POINT('Ctrl Pts',(19.0107666109437,21.7559951361578,8.38044385493705));
#139849=CARTESIAN_POINT('Ctrl Pts',(19.0982027560303,21.7464865106969,8.38483031694959));
#139850=CARTESIAN_POINT('Ctrl Pts',(19.1850129820694,21.7324815349687,8.38921677896212));
#139851=CARTESIAN_POINT('Ctrl Pts',(19.2707112385803,21.7141062794819,8.39360324097466));
#139852=CARTESIAN_POINT('Ctrl Pts',(19.352466391274,21.6965764967386,8.39778787536771));
#139853=CARTESIAN_POINT('Ctrl Pts',(19.4335139608229,21.6750045135588,8.40197250976077));
#139854=CARTESIAN_POINT('Ctrl Pts',(19.5134240199303,21.649462260761,8.40615714415381));
#139855=CARTESIAN_POINT('Ctrl Pts',(19.5932203369594,21.6239563641985,8.41033582223776));
#139856=CARTESIAN_POINT('Ctrl Pts',(19.671881925155,21.5944915619192,8.4145145003217));
#139857=CARTESIAN_POINT('Ctrl Pts',(19.7489895306432,21.5611906843243,8.41869317840565));
#139858=CARTESIAN_POINT('Ctrl Pts',(19.8274792345434,21.5272929124314,8.42294675629109));
#139859=CARTESIAN_POINT('Ctrl Pts',(19.9043582260683,21.489420290332,8.42720033417652));
#139860=CARTESIAN_POINT('Ctrl Pts',(19.9792009396775,21.447755377735,8.43145391206196));
#139861=CARTESIAN_POINT('Ctrl Pts',(20.0525926812398,21.4068982207711,8.43562502603991));
#139862=CARTESIAN_POINT('Ctrl Pts',(20.1240259742958,21.3623947371041,8.43979614001786));
#139863=CARTESIAN_POINT('Ctrl Pts',(20.1931217929876,21.3144646641265,8.44396725399581));
#139864=CARTESIAN_POINT('Ctrl Pts',(20.2621944259099,21.2665506745478,8.44813696831618));
#139865=CARTESIAN_POINT('Ctrl Pts',(20.3289307645448,21.215212641216,8.45230668263655));
#139866=CARTESIAN_POINT('Ctrl Pts',(20.3929803051521,21.1607139141724,8.45647639695692));
#139867=CARTESIAN_POINT('Ctrl Pts',(20.4570275666018,21.1062171264275,8.46064596290097));
#139868=CARTESIAN_POINT('Ctrl Pts',(20.5183878703047,21.0485601673606,8.464815528845));
#139869=CARTESIAN_POINT('Ctrl Pts',(20.5767444472639,20.9880461170375,8.46898509478905));
#139870=CARTESIAN_POINT('Ctrl Pts',(20.6371527694783,20.9254044673573,8.47330125752797));
#139871=CARTESIAN_POINT('Ctrl Pts',(20.6943418467815,20.859701457282,8.47761742026688));
#139872=CARTESIAN_POINT('Ctrl Pts',(20.7480039569823,20.7913126466809,8.48193358300581));
#139873=CARTESIAN_POINT('Ctrl Pts',(20.7999180295875,20.7251515943919,8.48610914719748));
#139874=CARTESIAN_POINT('Ctrl Pts',(20.8485311546646,20.6564774460931,8.49028471138917));
#139875=CARTESIAN_POINT('Ctrl Pts',(20.8936085817709,20.5856602393106,8.49446027558084));
#139876=CARTESIAN_POINT('Ctrl Pts',(20.940962762559,20.5112662237653,8.49884673759338));
#139877=CARTESIAN_POINT('Ctrl Pts',(20.9844143947686,20.4345074765788,8.50323319960592));
#139878=CARTESIAN_POINT('Ctrl Pts',(21.0237466725063,20.3558406770141,8.50761966161847));
#139879=CARTESIAN_POINT('Ctrl Pts',(21.0630789502441,20.2771738774495,8.51200612363101));
#139880=CARTESIAN_POINT('Ctrl Pts',(21.098291710861,20.1965995876304,8.51639258564355));
#139881=CARTESIAN_POINT('Ctrl Pts',(21.1292278697972,20.1145947386671,8.52077904765609));
#139882=CARTESIAN_POINT('Ctrl Pts',(21.1587406102023,20.0363630543649,8.52496368204914));
#139883=CARTESIAN_POINT('Ctrl Pts',(21.1844714983966,19.95653836908,8.52914831644219));
#139884=CARTESIAN_POINT('Ctrl Pts',(21.2062483053234,19.8755211184195,8.53333295083523));
#139885=CARTESIAN_POINT('Ctrl Pts',(21.227994115661,19.7946191857873,8.53751162891917));
#139886=CARTESIAN_POINT('Ctrl Pts',(21.2457969056054,19.7125284999515,8.54169030700312));
#139887=CARTESIAN_POINT('Ctrl Pts',(21.2595330219156,19.6296680728382,8.54586898508706));
#139888=CARTESIAN_POINT('Ctrl Pts',(21.2735153482386,19.5453224321195,8.5501225629725));
#139889=CARTESIAN_POINT('Ctrl Pts',(21.2832836065124,19.4601796345798,8.55437614085793));
#139890=CARTESIAN_POINT('Ctrl Pts',(21.288760950006,19.3746963295995,8.55862971874337));
#139891=CARTESIAN_POINT('Ctrl Pts',(21.2941321045079,19.2908702852932,8.56280083272132));
#139892=CARTESIAN_POINT('Ctrl Pts',(21.2953772042646,19.2067172987632,8.56697194669928));
#139893=CARTESIAN_POINT('Ctrl Pts',(21.2924758541409,19.1226750104568,8.57114306067723));
#139894=CARTESIAN_POINT('Ctrl Pts',(21.2895754775933,19.0386609233518,8.57531277499761));
#139895=CARTESIAN_POINT('Ctrl Pts',(21.2825314303294,18.9547579200746,8.57948248931798));
#139896=CARTESIAN_POINT('Ctrl Pts',(21.2713754270314,18.8714032651847,8.58365220363836));
#139897=CARTESIAN_POINT('Ctrl Pts',(21.2602198207119,18.7880515764115,8.58782176958239));
#139898=CARTESIAN_POINT('Ctrl Pts',(21.2449526111525,18.7052486530838,8.59199133552643));
#139899=CARTESIAN_POINT('Ctrl Pts',(21.2256571796749,18.6234248992897,8.59616090147046));
#139900=CARTESIAN_POINT('Ctrl Pts',(21.20568334463,18.5387243232526,8.60047706420938));
#139901=CARTESIAN_POINT('Ctrl Pts',(21.181392873751,18.4550735664106,8.60479322694831));
#139902=CARTESIAN_POINT('Ctrl Pts',(21.1529349892687,18.3729346578627,8.60910938968723));
#139903=CARTESIAN_POINT('Ctrl Pts',(21.1254041173801,18.2934714156214,8.61328495387891));
#139904=CARTESIAN_POINT('Ctrl Pts',(21.0939733891638,18.2154234566595,8.61746051807059));
#139905=CARTESIAN_POINT('Ctrl Pts',(21.0588268816573,18.1391884632437,8.62163608226227));
#139906=CARTESIAN_POINT('Ctrl Pts',(21.0219052076094,18.0591030215419,8.62602254427481));
#139907=CARTESIAN_POINT('Ctrl Pts',(20.9808827929503,17.9810190212162,8.63040900628736));
#139908=CARTESIAN_POINT('Ctrl Pts',(20.9360262797511,17.9053659535362,8.6347954682999));
#139909=CARTESIAN_POINT('Ctrl Pts',(20.891169766552,17.8297128858561,8.63918193031245));
#139910=CARTESIAN_POINT('Ctrl Pts',(20.842479539431,17.7564911918507,8.64356839232499));
#139911=CARTESIAN_POINT('Ctrl Pts',(20.790271595083,17.6860911085397,8.64795485433753));
#139912=CARTESIAN_POINT('Ctrl Pts',(20.7404694331042,17.6189351154018,8.65213918479511));
#139913=CARTESIAN_POINT('Ctrl Pts',(20.6872812569781,17.5540964632771,8.65632351525269));
#139914=CARTESIAN_POINT('Ctrl Pts',(20.6309504906906,17.4919366399494,8.66050784571027));
#139915=CARTESIAN_POINT('Ctrl Pts',(20.5747060923848,17.4298721218843,8.66468576062977));
#139916=CARTESIAN_POINT('Ctrl Pts',(20.5153289851675,17.3704786083014,8.66886367554927));
#139917=CARTESIAN_POINT('Ctrl Pts',(20.4531043975747,17.3140866993351,8.67304159046877));
#139918=CARTESIAN_POINT('Ctrl Pts',(20.4017904485504,17.2675827102526,8.67648693774226));
#139919=CARTESIAN_POINT('Ctrl Pts',(20.3485409039237,17.2231195485426,8.67993228501575));
#139920=CARTESIAN_POINT('Ctrl Pts',(20.2935357313021,17.1808649545431,8.68337763228924));
#139921=CARTESIAN_POINT('Origin',(18.734,19.211,-1.76670989022852));
#139922=CARTESIAN_POINT('',(20.2954164566376,17.1783794293288,9.5499633233039));
#139923=CARTESIAN_POINT('',(20.2935357313021,17.1808649545431,9.48328065833267));
#139924=CARTESIAN_POINT('',(20.2935357313021,17.1808649545432,-1.76670989022852));
#139925=CARTESIAN_POINT('',(16.1736699135442,19.2103574886798,9.03329016588334));
#139926=CARTESIAN_POINT('Ctrl Pts',(16.1699656655267,19.2103691596404,9.03329079541918));
#139927=CARTESIAN_POINT('Ctrl Pts',(16.1727141287504,20.0241270866321,9.07394170533784));
#139928=CARTESIAN_POINT('Ctrl Pts',(17.0319371680896,21.691475877328,9.15698455081697));
#139929=CARTESIAN_POINT('Ctrl Pts',(19.8732646807496,22.0155260890916,9.28241933185656));
#139930=CARTESIAN_POINT('Ctrl Pts',(21.7088249788763,19.7710954760151,9.40959513853801));
#139931=CARTESIAN_POINT('Ctrl Pts',(21.0821529672139,17.8368644753459,9.49877646902045));
#139932=CARTESIAN_POINT('Ctrl Pts',(20.3656977297167,17.2315280348845,9.54556586394241));
#139933=CARTESIAN_POINT('Ctrl Pts',(20.2954164566376,17.1783794293288,9.5499633233039));
#139934=CARTESIAN_POINT('Ctrl Pts',(20.2935357313021,17.1808649545431,8.74981199697633));
#139935=CARTESIAN_POINT('Ctrl Pts',(20.2268660954868,17.1296498004185,8.75399550841146));
#139936=CARTESIAN_POINT('Ctrl Pts',(20.1577482403935,17.0817815617839,8.75817901984659));
#139937=CARTESIAN_POINT('Ctrl Pts',(20.086560133894,17.0374818647638,8.76236253128172));
#139938=CARTESIAN_POINT('Ctrl Pts',(20.0221613278628,16.9974070863223,8.76614705589809));
#139939=CARTESIAN_POINT('Ctrl Pts',(19.9560688916324,16.9602521636411,8.76993158051446));
#139940=CARTESIAN_POINT('Ctrl Pts',(19.8885775886028,16.9261475776549,8.77371610513083));
#139941=CARTESIAN_POINT('Ctrl Pts',(19.8139509296381,16.8884373662162,8.77790073952388));
#139942=CARTESIAN_POINT('Ctrl Pts',(19.7373359438749,16.8543169479217,8.78208537391693));
#139943=CARTESIAN_POINT('Ctrl Pts',(19.6591123506695,16.8240003898955,8.78627000830997));
#139944=CARTESIAN_POINT('Ctrl Pts',(19.5810000990668,16.7937269837373,8.79044868639392));
#139945=CARTESIAN_POINT('Ctrl Pts',(19.5012842132702,16.7672468481168,8.79462736447787));
#139946=CARTESIAN_POINT('Ctrl Pts',(19.420368077509,16.7447277396491,8.79880604256181));
#139947=CARTESIAN_POINT('Ctrl Pts',(19.3380015781677,16.7218049923462,8.80305962044725));
#139948=CARTESIAN_POINT('Ctrl Pts',(19.2543918069889,16.7029868892007,8.80731319833268));
#139949=CARTESIAN_POINT('Ctrl Pts',(19.1699845756622,16.6883986740302,8.81156677621811));
#139950=CARTESIAN_POINT('Ctrl Pts',(19.0872137432219,16.6740932798773,8.81573789019606));
#139951=CARTESIAN_POINT('Ctrl Pts',(19.0036765695344,16.6638553099793,8.81990900417402));
#139952=CARTESIAN_POINT('Ctrl Pts',(18.9198060037776,16.6577518473599,8.82408011815197));
#139953=CARTESIAN_POINT('Ctrl Pts',(18.8359635815991,16.6516504328162,8.82824983247234));
#139954=CARTESIAN_POINT('Ctrl Pts',(18.7517884479705,16.6496808035662,8.83241954679272));
#139955=CARTESIAN_POINT('Ctrl Pts',(18.6677187513895,16.6518581914863,8.83658926111309));
#139956=CARTESIAN_POINT('Ctrl Pts',(18.5836520463691,16.6540355019256,8.84075882705714));
#139957=CARTESIAN_POINT('Ctrl Pts',(18.4996912307931,16.660359523368,8.84492839300118));
#139958=CARTESIAN_POINT('Ctrl Pts',(18.4162731576902,16.6707933836643,8.84909795894523));
#139959=CARTESIAN_POINT('Ctrl Pts',(18.3299222080443,16.681594085617,8.85341412168415));
#139960=CARTESIAN_POINT('Ctrl Pts',(18.2441533999762,16.6967989420232,8.85773028442307));
#139961=CARTESIAN_POINT('Ctrl Pts',(18.1594420717103,16.7163089996876,8.86204644716199));
#139962=CARTESIAN_POINT('Ctrl Pts',(18.0774902060527,16.7351835192758,8.86622201135367));
#139963=CARTESIAN_POINT('Ctrl Pts',(17.996528423794,16.758086889941,8.87039757554535));
#139964=CARTESIAN_POINT('Ctrl Pts',(17.9169718130409,16.7848786218092,8.87457313973703));
#139965=CARTESIAN_POINT('Ctrl Pts',(17.8333969870066,16.8130235403628,8.87895960174957));
#139966=CARTESIAN_POINT('Ctrl Pts',(17.7513735563979,16.8454597306831,8.88334606376211));
#139967=CARTESIAN_POINT('Ctrl Pts',(17.6713570660694,16.8819680133224,8.88773252577465));
#139968=CARTESIAN_POINT('Ctrl Pts',(17.5913405757408,16.9184762959617,8.89211898778719));
#139969=CARTESIAN_POINT('Ctrl Pts',(17.513331505326,16.959056335675,8.89650544979973));
#139970=CARTESIAN_POINT('Ctrl Pts',(17.4377516489576,17.003435683288,8.90089191181227));
#139971=CARTESIAN_POINT('Ctrl Pts',(17.365649333817,17.0457730713314,8.90507654620532));
#139972=CARTESIAN_POINT('Ctrl Pts',(17.2954892230291,17.091725414496,8.90926118059837));
#139973=CARTESIAN_POINT('Ctrl Pts',(17.2276568480541,17.1410892993693,8.91344581499142));
#139974=CARTESIAN_POINT('Ctrl Pts',(17.159921024069,17.1903829208624,8.91762449307535));
#139975=CARTESIAN_POINT('Ctrl Pts',(17.0945067235342,17.2430781703289,8.92180317115929));
#139976=CARTESIAN_POINT('Ctrl Pts',(17.0317733474474,17.2989266689429,8.92598184924323));
#139977=CARTESIAN_POINT('Ctrl Pts',(16.9679155206799,17.3557762117571,8.93023542712867));
#139978=CARTESIAN_POINT('Ctrl Pts',(16.9068360906096,17.4158929154663,8.9344890050141));
#139979=CARTESIAN_POINT('Ctrl Pts',(16.8488816768788,17.4789697150936,8.93874258289954));
#139980=CARTESIAN_POINT('Ctrl Pts',(16.792050822547,17.540823647876,8.94291369687749));
#139981=CARTESIAN_POINT('Ctrl Pts',(16.7382252223475,17.6055235719755,8.94708481085544));
#139982=CARTESIAN_POINT('Ctrl Pts',(16.6876956296653,17.6727417564176,8.9512559248334));
#139983=CARTESIAN_POINT('Ctrl Pts',(16.637182992676,17.7399373851488,8.95542563915377));
#139984=CARTESIAN_POINT('Ctrl Pts',(16.5899644428518,17.8096492285707,8.95959535347414));
#139985=CARTESIAN_POINT('Ctrl Pts',(16.5462899492621,17.8815171178611,8.96376506779451));
#139986=CARTESIAN_POINT('Ctrl Pts',(16.5026170097983,17.9533824497836,8.96793463373855));
#139987=CARTESIAN_POINT('Ctrl Pts',(16.4624881140049,18.0274032814579,8.9721041996826));
#139988=CARTESIAN_POINT('Ctrl Pts',(16.4261087184981,18.1031923304257,8.97627376562664));
#139989=CARTESIAN_POINT('Ctrl Pts',(16.3884502683242,18.1816460288594,8.98058992836556));
#139990=CARTESIAN_POINT('Ctrl Pts',(16.3548101172679,18.2619941236263,8.98490609110448));
#139991=CARTESIAN_POINT('Ctrl Pts',(16.3253623529172,18.3437833690158,8.9892222538434));
#139992=CARTESIAN_POINT('Ctrl Pts',(16.296873846393,18.4229083383394,8.99339781803508));
#139993=CARTESIAN_POINT('Ctrl Pts',(16.2723088794104,18.5033815448835,8.99757338222676));
#139994=CARTESIAN_POINT('Ctrl Pts',(16.2517740015379,18.5847779207351,9.00174894641844));
#139995=CARTESIAN_POINT('Ctrl Pts',(16.2302019558011,18.6702854340295,9.00613540843099));
#139996=CARTESIAN_POINT('Ctrl Pts',(16.213077931431,18.7568112533014,9.01052187044352));
#139997=CARTESIAN_POINT('Ctrl Pts',(16.2004642109876,18.8438536997419,9.01490833245606));
#139998=CARTESIAN_POINT('Ctrl Pts',(16.1878504905441,18.9308961461825,9.01929479446861));
#139999=CARTESIAN_POINT('Ctrl Pts',(16.179747051756,19.0184546350337,9.02368125648115));
#140000=CARTESIAN_POINT('Ctrl Pts',(16.1761531171477,19.10602703261,9.02806771849369));
#140001=CARTESIAN_POINT('Ctrl Pts',(16.1747268399112,19.1407807303868,9.0298085155863));
#140002=CARTESIAN_POINT('Ctrl Pts',(16.1740088273484,19.1755636940745,9.0315493126789));
#140003=CARTESIAN_POINT('Ctrl Pts',(16.1740000808904,19.2103564484228,9.0332901097715));
#140004=CARTESIAN_POINT('',(16.174000001606,19.2110906788005,8.96670989026365));
#140005=CARTESIAN_POINT('Ctrl Pts',(20.2935357313021,17.1808649545431,8.68337763228924));
#140006=CARTESIAN_POINT('Ctrl Pts',(20.2269370011896,17.1297042696901,8.68754916275219));
#140007=CARTESIAN_POINT('Ctrl Pts',(20.157763917459,17.0817825471759,8.69172069321514));
#140008=CARTESIAN_POINT('Ctrl Pts',(20.0863673947936,17.0373619368673,8.69589222367809));
#140009=CARTESIAN_POINT('Ctrl Pts',(20.0149989840445,16.9929588168851,8.70006211162806));
#140010=CARTESIAN_POINT('Ctrl Pts',(19.9414092630416,16.9520543143202,8.70423199957803));
#140011=CARTESIAN_POINT('Ctrl Pts',(19.8659780913813,16.9148672510865,8.70840188752799));
#140012=CARTESIAN_POINT('Ctrl Pts',(19.7905539926854,16.8776836747771,8.71257138447953));
#140013=CARTESIAN_POINT('Ctrl Pts',(19.7132891992873,16.8442170480217,8.71674088143107));
#140014=CARTESIAN_POINT('Ctrl Pts',(19.6345869032211,16.8146395868429,8.72091037838262));
#140015=CARTESIAN_POINT('Ctrl Pts',(19.5558683784269,16.7850560266733,8.7250807351011));
#140016=CARTESIAN_POINT('Ctrl Pts',(19.4757121933861,16.7593633850936,8.72925109181958));
#140017=CARTESIAN_POINT('Ctrl Pts',(19.3945388869154,16.7376847392876,8.73342144853806));
#140018=CARTESIAN_POINT('Ctrl Pts',(19.3132745110844,16.7159817719345,8.73759648403255));
#140019=CARTESIAN_POINT('Ctrl Pts',(19.2309911818684,16.6983019051782,8.74177151952703));
#140020=CARTESIAN_POINT('Ctrl Pts',(19.1481213253207,16.6847174489154,8.74594655502151));
#140021=CARTESIAN_POINT('Ctrl Pts',(19.0651969677462,16.6711240585619,8.75012433631201));
#140022=CARTESIAN_POINT('Ctrl Pts',(18.9816857717183,16.6616314907568,8.75430211760251));
#140023=CARTESIAN_POINT('Ctrl Pts',(18.8980246357382,16.6562601073943,8.75847989889301));
#140024=CARTESIAN_POINT('Ctrl Pts',(18.8142288636417,16.6508800798485,8.76266440349943));
#140025=CARTESIAN_POINT('Ctrl Pts',(18.7302831289701,16.6496344772916,8.76684890810586));
#140026=CARTESIAN_POINT('Ctrl Pts',(18.6466231447615,16.6524915897796,8.77103341271229));
#140027=CARTESIAN_POINT('Ctrl Pts',(18.6193179827511,16.6534241015426,8.77239916214785));
#140028=CARTESIAN_POINT('Ctrl Pts',(18.5920432050038,16.6547932470753,8.77376491158341));
#140029=CARTESIAN_POINT('Ctrl Pts',(18.5648137584889,16.6565967398072,8.77513066101897));
#140030=CARTESIAN_POINT('Ctrl Pts',(18.4813831705471,16.6621226126484,8.77931529541201));
#140031=CARTESIAN_POINT('Ctrl Pts',(18.3980683312295,16.6717505167586,8.78349992980505));
#140032=CARTESIAN_POINT('Ctrl Pts',(18.3153050503469,16.6854714337124,8.7876845641981));
#140033=CARTESIAN_POINT('Ctrl Pts',(18.2326595727503,16.6991728206391,8.79186324228205));
#140034=CARTESIAN_POINT('Ctrl Pts',(18.150564544139,16.7169555737483,8.796041920366));
#140035=CARTESIAN_POINT('Ctrl Pts',(18.0694525718374,16.738758766681,8.80022059844995));
#140036=CARTESIAN_POINT('Ctrl Pts',(17.9868867257265,16.7609527661774,8.80447417633538));
#140037=CARTESIAN_POINT('Ctrl Pts',(17.9053400062234,16.7873127240842,8.80872775422082));
#140038=CARTESIAN_POINT('Ctrl Pts',(17.8252599013638,16.8177195247672,8.81298133210625));
#140039=CARTESIAN_POINT('Ctrl Pts',(17.7467323056004,16.8475368302849,8.8171524460842));
#140040=CARTESIAN_POINT('Ctrl Pts',(17.6696154154523,16.8812452961237,8.82132356006215));
#140041=CARTESIAN_POINT('Ctrl Pts',(17.5943160431835,16.9186822910916,8.8254946740401));
#140042=CARTESIAN_POINT('Ctrl Pts',(17.5190419383462,16.9561067237143,8.82966438836047));
#140043=CARTESIAN_POINT('Ctrl Pts',(17.4455845517329,16.9972569960431,8.83383410268084));
#140044=CARTESIAN_POINT('Ctrl Pts',(17.3743287784396,17.0419231988562,8.83800381700122));
#140045=CARTESIAN_POINT('Ctrl Pts',(17.3030755407325,17.086587812254,8.84217338294526));
#140046=CARTESIAN_POINT('Ctrl Pts',(17.2340241499107,17.1347678623261,8.8463429488893));
#140047=CARTESIAN_POINT('Ctrl Pts',(17.1675318647116,17.1862092500394,8.85051251483334));
#140048=CARTESIAN_POINT('Ctrl Pts',(17.0987017927918,17.239459253485,8.85482867757226));
#140049=CARTESIAN_POINT('Ctrl Pts',(17.0326145482172,17.2962038761403,8.85914484031118));
#140050=CARTESIAN_POINT('Ctrl Pts',(16.9696289167233,17.3561159927108,8.86346100305011));
#140051=CARTESIAN_POINT('Ctrl Pts',(16.9086950355505,17.4140764783858,8.86763656724179));
#140052=CARTESIAN_POINT('Ctrl Pts',(16.8506640912072,17.4750008911688,8.87181213143347));
#140053=CARTESIAN_POINT('Ctrl Pts',(16.7958218659393,17.5385570202099,8.87598769562515));
#140054=CARTESIAN_POINT('Ctrl Pts',(16.7382096902482,17.6053232182385,8.88037415763769));
#140055=CARTESIAN_POINT('Ctrl Pts',(16.6841171816931,17.6749935141295,8.88476061965023));
#140056=CARTESIAN_POINT('Ctrl Pts',(16.6338248927155,17.7471473712348,8.88914708166278));
#140057=CARTESIAN_POINT('Ctrl Pts',(16.5835326037379,17.8193012283401,8.89353354367532));
#140058=CARTESIAN_POINT('Ctrl Pts',(16.5370407765469,17.8939381139568,8.89792000568786));
#140059=CARTESIAN_POINT('Ctrl Pts',(16.4945737975988,17.9706088181549,8.9023064677004));
#140060=CARTESIAN_POINT('Ctrl Pts',(16.4520961746313,18.0472987392713,8.90669402914567));
#140061=CARTESIAN_POINT('Ctrl Pts',(16.4134992022808,18.1262856298358,8.91108159059094));
#140062=CARTESIAN_POINT('Ctrl Pts',(16.3790251742671,18.2071605854698,8.91546915203621));
#140063=CARTESIAN_POINT('Ctrl Pts',(16.3446454932945,18.2878142059945,8.91984470579152));
#140064=CARTESIAN_POINT('Ctrl Pts',(16.3143664333072,18.3703452363826,8.92422025954683));
#140065=CARTESIAN_POINT('Ctrl Pts',(16.2883841141658,18.4543211123896,8.92859581330214));
#140066=CARTESIAN_POINT('Ctrl Pts',(16.2624439986578,18.5381605845957,8.93296425975245));
#140067=CARTESIAN_POINT('Ctrl Pts',(16.2407868563187,18.6234398583863,8.93733270620276));
#140068=CARTESIAN_POINT('Ctrl Pts',(16.2235607960525,18.7097066694205,8.94170115265307));
#140069=CARTESIAN_POINT('Ctrl Pts',(16.2063704951607,18.7957944002037,8.94606053069715));
#140070=CARTESIAN_POINT('Ctrl Pts',(16.193593030381,18.8828651985171,8.95041990874122));
#140071=CARTESIAN_POINT('Ctrl Pts',(16.1853263642748,18.9704533339262,8.9547792867853));
#140072=CARTESIAN_POINT('Ctrl Pts',(16.1777850503447,19.0503561166421,8.9587561545997));
#140073=CARTESIAN_POINT('Ctrl Pts',(16.1739971536887,19.1306890276032,8.96273302241411));
#140074=CARTESIAN_POINT('Ctrl Pts',(16.174000001606,19.21109067809,8.96670989022851));
#140075=CARTESIAN_POINT('Ctrl Pts',(16.174000001606,19.2110906788005,8.96670989026365));
#140076=CARTESIAN_POINT('Ctrl Pts',(16.1740031377284,19.2996281672636,8.97108917708311));
#140077=CARTESIAN_POINT('Ctrl Pts',(16.1786036643305,19.388071802769,8.97546846390256));
#140078=CARTESIAN_POINT('Ctrl Pts',(16.1877467776184,19.4759424985001,8.97984775072202));
#140079=CARTESIAN_POINT('Ctrl Pts',(16.1969159526896,19.5640636632955,8.98423952038188));
#140080=CARTESIAN_POINT('Ctrl Pts',(16.2106535575187,19.6516082364872,8.98863129004175));
#140081=CARTESIAN_POINT('Ctrl Pts',(16.2288531973791,19.7381048257399,8.99302305970162));
#140082=CARTESIAN_POINT('Ctrl Pts',(16.2470794228643,19.8247277672657,8.99742124475987));
#140083=CARTESIAN_POINT('Ctrl Pts',(16.2697805833341,19.9102992971043,9.00181942981813));
#140084=CARTESIAN_POINT('Ctrl Pts',(16.2968004138021,19.9943633748375,9.00621761487638));
#140085=CARTESIAN_POINT('Ctrl Pts',(16.3238953969119,20.0786612674176,9.01062803299533));
#140086=CARTESIAN_POINT('Ctrl Pts',(16.3553329301083,20.1614429605719,9.01503845111429));
#140087=CARTESIAN_POINT('Ctrl Pts',(16.3909082116845,20.2422714829415,9.01944886923325));
#140088=CARTESIAN_POINT('Ctrl Pts',(16.4178853374884,20.3035646370615,9.02279333761611));
#140089=CARTESIAN_POINT('Ctrl Pts',(16.4472408225494,20.363735085321,9.02613780599897));
#140090=CARTESIAN_POINT('Ctrl Pts',(16.478868382946,20.422602818486,9.02948227438183));
#140091=CARTESIAN_POINT('Ctrl Pts',(16.5184411227219,20.4962587519986,9.03366690877488));
#140092=CARTESIAN_POINT('Ctrl Pts',(16.5616998679758,20.5681109610611,9.03785154316793));
#140093=CARTESIAN_POINT('Ctrl Pts',(16.6084559713663,20.6377664778581,9.04203617756098));
#140094=CARTESIAN_POINT('Ctrl Pts',(16.6551455232309,20.7073228486487,9.04621485564492));
#140095=CARTESIAN_POINT('Ctrl Pts',(16.7053222910481,20.7746883591286,9.05039353372887));
#140096=CARTESIAN_POINT('Ctrl Pts',(16.7587517035101,20.8394944480144,9.05457221181282));
#140097=CARTESIAN_POINT('Ctrl Pts',(16.8131387997914,20.9054621394682,9.05882578969825));
#140098=CARTESIAN_POINT('Ctrl Pts',(16.8708960667842,20.9687773268414,9.06307936758369));
#140099=CARTESIAN_POINT('Ctrl Pts',(16.9317298045576,21.0290819955712,9.06733294546912));
#140100=CARTESIAN_POINT('Ctrl Pts',(16.9913841616171,21.0882175406228,9.07150405944708));
#140101=CARTESIAN_POINT('Ctrl Pts',(17.0539964254171,21.1444579161298,9.07567517342503));
#140102=CARTESIAN_POINT('Ctrl Pts',(17.1192501263854,21.1975001499274,9.07984628740298));
#140103=CARTESIAN_POINT('Ctrl Pts',(17.1844819308442,21.2505245848913,9.08401600172335));
#140104=CARTESIAN_POINT('Ctrl Pts',(17.2523530554692,21.3003527195435,9.08818571604373));
#140105=CARTESIAN_POINT('Ctrl Pts',(17.3225130695873,21.3467211066228,9.0923554303641));
#140106=CARTESIAN_POINT('Ctrl Pts',(17.3926705871109,21.3930878437158,9.09652499630815));
#140107=CARTESIAN_POINT('Ctrl Pts',(17.4651164479275,21.4359948250818,9.10069456225219));
#140108=CARTESIAN_POINT('Ctrl Pts',(17.5394714392698,21.475222055718,9.10486412819623));
#140109=CARTESIAN_POINT('Ctrl Pts',(17.6164406603808,21.5158284673913,9.10918029093515));
#140110=CARTESIAN_POINT('Ctrl Pts',(17.6954552934394,21.5524913076844,9.11349645367408));
#140111=CARTESIAN_POINT('Ctrl Pts',(17.7760690203244,21.5850194266639,9.117812616413));
#140112=CARTESIAN_POINT('Ctrl Pts',(17.8540567635352,21.6164879455891,9.12198818060468));
#140113=CARTESIAN_POINT('Ctrl Pts',(17.9335405590284,21.6440868736176,9.12616374479636));
#140114=CARTESIAN_POINT('Ctrl Pts',(18.0140996850996,21.6676936187906,9.13033930898804));
#140115=CARTESIAN_POINT('Ctrl Pts',(18.0987276611175,21.6924926845425,9.13472577100058));
#140116=CARTESIAN_POINT('Ctrl Pts',(18.1845418843915,21.7128855434687,9.13911223301312));
#140117=CARTESIAN_POINT('Ctrl Pts',(18.2710433987722,21.7287909336122,9.14349869502566));
#140118=CARTESIAN_POINT('Ctrl Pts',(18.3575449131529,21.7446963237556,9.14788515703819));
#140119=CARTESIAN_POINT('Ctrl Pts',(18.4447331334585,21.756114245197,9.15227161905073));
#140120=CARTESIAN_POINT('Ctrl Pts',(18.5321062576865,21.7630264334083,9.15665808106327));
#140121=CARTESIAN_POINT('Ctrl Pts',(18.6154592149507,21.7696205815937,9.16084271545632));
#140122=CARTESIAN_POINT('Ctrl Pts',(18.6992906902526,21.7721390606606,9.16502734984937));
#140123=CARTESIAN_POINT('Ctrl Pts',(18.78316814862,21.7705277871438,9.16921198424242));
#140124=CARTESIAN_POINT('Ctrl Pts',(18.8669262178074,21.7689188070754,9.17339066232636));
#140125=CARTESIAN_POINT('Ctrl Pts',(18.9507296840396,21.7631917591217,9.17756934041031));
#140126=CARTESIAN_POINT('Ctrl Pts',(19.0341416766033,21.7533443853982,9.18174801849425));
#140127=CARTESIAN_POINT('Ctrl Pts',(19.1190487691866,21.7433205045779,9.18600159637969));
#140128=CARTESIAN_POINT('Ctrl Pts',(19.2035497350918,21.7290270933803,9.19025517426511));
#140129=CARTESIAN_POINT('Ctrl Pts',(19.2871845665266,21.7105173204755,9.19450875215055));
#140130=CARTESIAN_POINT('Ctrl Pts',(19.369197973554,21.6923663956372,9.1986798661285));
#140131=CARTESIAN_POINT('Ctrl Pts',(19.4503780599824,21.6701612389659,9.20285098010646));
#140132=CARTESIAN_POINT('Ctrl Pts',(19.5302987751906,21.6440039582027,9.20702209408442));
#140133=CARTESIAN_POINT('Ctrl Pts',(19.610192672231,21.6178554547677,9.21119180840479));
#140134=CARTESIAN_POINT('Ctrl Pts',(19.6888276004821,21.5877576040183,9.21536152272516));
#140135=CARTESIAN_POINT('Ctrl Pts',(19.7657923610116,21.553862463688,9.21953123704553));
#140136=CARTESIAN_POINT('Ctrl Pts',(19.8427543828046,21.5199685294922,9.22370080298957));
#140137=CARTESIAN_POINT('Ctrl Pts',(19.9180459343718,21.4822777605697,9.22787036893362));
#140138=CARTESIAN_POINT('Ctrl Pts',(19.9912767740527,21.4409899357234,9.23203993487766));
#140139=CARTESIAN_POINT('Ctrl Pts',(20.0670823197166,21.3982504818896,9.23635609761658));
#140140=CARTESIAN_POINT('Ctrl Pts',(20.1406790886265,21.351656579909,9.2406722603555));
#140141=CARTESIAN_POINT('Ctrl Pts',(20.2116647704044,21.3014800468566,9.24498842309442));
#140142=CARTESIAN_POINT('Ctrl Pts',(20.2803381010648,21.2529380090908,9.2491639872861));
#140143=CARTESIAN_POINT('Ctrl Pts',(20.3465675028829,21.2010434919511,9.25333955147778));
#140144=CARTESIAN_POINT('Ctrl Pts',(20.4100221667426,21.1460838991081,9.25751511566946));
#140145=CARTESIAN_POINT('Ctrl Pts',(20.4766817748247,21.0883484278846,9.26190157768201));
#140146=CARTESIAN_POINT('Ctrl Pts',(20.5402785534045,21.0272305142621,9.26628803969455));
#140147=CARTESIAN_POINT('Ctrl Pts',(20.6004740985359,20.9631057158444,9.27067450170709));
#140148=CARTESIAN_POINT('Ctrl Pts',(20.6606696436673,20.8989809174267,9.27506096371963));
#140149=CARTESIAN_POINT('Ctrl Pts',(20.7174636386703,20.8318497263029,9.27944742573217));
#140150=CARTESIAN_POINT('Ctrl Pts',(20.7705691100607,20.7621241923026,9.28383388774471));
#140151=CARTESIAN_POINT('Ctrl Pts',(20.8212311199913,20.6956068334797,9.28801852213775));
#140152=CARTESIAN_POINT('Ctrl Pts',(20.8687251499198,20.6264810343217,9.2922031565308));
#140153=CARTESIAN_POINT('Ctrl Pts',(20.9127716012342,20.5550812139358,9.29638779092385));
#140154=CARTESIAN_POINT('Ctrl Pts',(20.9567553578771,20.4837830223568,9.30056646900779));
#140155=CARTESIAN_POINT('Ctrl Pts',(20.997301043686,20.4102176270062,9.30474514709174));
#140156=CARTESIAN_POINT('Ctrl Pts',(21.0341702903064,20.3347511448678,9.30892382517568));
#140157=CARTESIAN_POINT('Ctrl Pts',(21.071700391675,20.2579319802738,9.31317740306111));
#140158=CARTESIAN_POINT('Ctrl Pts',(21.1054206649962,20.1791432881301,9.31743098094655));
#140159=CARTESIAN_POINT('Ctrl Pts',(21.1351268232138,20.0988006413847,9.32168455883199));
#140160=CARTESIAN_POINT('Ctrl Pts',(21.1642570695876,20.0200155936223,9.32585567280994));
#140161=CARTESIAN_POINT('Ctrl Pts',(21.1895272879509,19.9397367578111,9.33002678678789));
#140162=CARTESIAN_POINT('Ctrl Pts',(21.2107927216344,19.8583776440833,9.33419790076584));
#140163=CARTESIAN_POINT('Ctrl Pts',(21.2320510194963,19.777045831192,9.33836761508621));
#140164=CARTESIAN_POINT('Ctrl Pts',(21.2493070853372,19.6946349050203,9.34253732940659));
#140165=CARTESIAN_POINT('Ctrl Pts',(21.2624662014641,19.6115729247638,9.34670704372696));
#140166=CARTESIAN_POINT('Ctrl Pts',(21.2756248493332,19.528513900209,9.350876609671));
#140167=CARTESIAN_POINT('Ctrl Pts',(21.284686766209,19.4448043221315,9.35504617561504));
#140168=CARTESIAN_POINT('Ctrl Pts',(21.2896087040397,19.3608804584879,9.35921574155908));
#140169=CARTESIAN_POINT('Ctrl Pts',(21.2947036911327,19.2740059353298,9.36353190429801));
#140170=CARTESIAN_POINT('Ctrl Pts',(21.2953621283496,19.1869023041989,9.36784806703693));
#140171=CARTESIAN_POINT('Ctrl Pts',(21.2915948078576,19.1000549738833,9.37216422977585));
#140172=CARTESIAN_POINT('Ctrl Pts',(21.2879502074343,19.016036686218,9.37633979396753));
#140173=CARTESIAN_POINT('Ctrl Pts',(21.2801638500694,18.9322587224487,9.38051535815921));
#140174=CARTESIAN_POINT('Ctrl Pts',(21.2682983360669,18.8491548068462,9.38469092235089));
#140175=CARTESIAN_POINT('Ctrl Pts',(21.2558335231598,18.7618535100274,9.38907738436343));
#140176=CARTESIAN_POINT('Ctrl Pts',(21.2388667599596,18.6752967161991,9.39346384637597));
#140177=CARTESIAN_POINT('Ctrl Pts',(21.2175306593405,18.5899722517346,9.39785030838851));
#140178=CARTESIAN_POINT('Ctrl Pts',(21.1961945587214,18.5046477872701,9.40223677040106));
#140179=CARTESIAN_POINT('Ctrl Pts',(21.1704893630394,18.4205561848056,9.4066232324136));
#140180=CARTESIAN_POINT('Ctrl Pts',(21.1406062076889,18.3381617783842,9.41100969442614));
#140181=CARTESIAN_POINT('Ctrl Pts',(21.1121004746698,18.259565227111,9.41519396859536));
#140182=CARTESIAN_POINT('Ctrl Pts',(21.0796873621586,18.182220330688,9.41937824276457));
#140183=CARTESIAN_POINT('Ctrl Pts',(21.0434966865738,18.1065430951347,9.42356251693379));
#140184=CARTESIAN_POINT('Ctrl Pts',(21.007355056005,18.0309684161425,9.42774112064258));
#140185=CARTESIAN_POINT('Ctrl Pts',(20.9674462242518,17.9570573217824,9.43191972435137));
#140186=CARTESIAN_POINT('Ctrl Pts',(20.9239489993286,17.8852083948299,9.43609832806016));
#140187=CARTESIAN_POINT('Ctrl Pts',(20.8805019784934,17.8134423952331,9.44027210886385));
#140188=CARTESIAN_POINT('Ctrl Pts',(20.8334750334886,17.7437342236849,9.44444588966753));
#140189=CARTESIAN_POINT('Ctrl Pts',(20.7830933894016,17.6764589345635,9.44861967047122));
#140190=CARTESIAN_POINT('Ctrl Pts',(20.7327462827087,17.6092297636906,9.45279059008379));
#140191=CARTESIAN_POINT('Ctrl Pts',(20.6790493196799,17.5444305296965,9.45696150969635));
#140192=CARTESIAN_POINT('Ctrl Pts',(20.6222709998958,17.4824073264784,9.46113242930892));
#140193=CARTESIAN_POINT('Ctrl Pts',(20.5655043373565,17.4203968573402,9.46530249258352));
#140194=CARTESIAN_POINT('Ctrl Pts',(20.5056578783566,17.3611616320062,9.46947255585812));
#140195=CARTESIAN_POINT('Ctrl Pts',(20.4430396423748,17.3050137721402,9.47364261913271));
#140196=CARTESIAN_POINT('Ctrl Pts',(20.3947976075597,17.2617566128161,9.47685529886603));
#140197=CARTESIAN_POINT('Ctrl Pts',(20.3449112621541,17.2203312827846,9.48006797859935));
#140198=CARTESIAN_POINT('Ctrl Pts',(20.2935357313021,17.1808649545431,9.48328065833267));
#140199=CARTESIAN_POINT('Origin',(18.734,19.211,-1.76670989022852));
#140200=CARTESIAN_POINT('',(20.2935357313021,17.1808649545432,10.3499274784722));
#140201=CARTESIAN_POINT('',(20.2935357313021,17.1808649545432,10.2832382208556));
#140202=CARTESIAN_POINT('',(20.2935357313021,17.1808649545432,-1.76670989022852));
#140203=CARTESIAN_POINT('',(16.1740007840082,19.2089964727374,9.83329010977151));
#140204=CARTESIAN_POINT('Ctrl Pts',(16.1740007840082,19.2089964727374,9.83329010977151));
#140205=CARTESIAN_POINT('Ctrl Pts',(16.1739350379054,19.2930033015151,9.83745593779553));
#140206=CARTESIAN_POINT('Ctrl Pts',(16.1780086491546,19.3770604200798,9.84162176581954));
#140207=CARTESIAN_POINT('Ctrl Pts',(16.186209790272,19.4607299485725,9.84578759384356));
#140208=CARTESIAN_POINT('Ctrl Pts',(16.1944094741073,19.544384609609,9.84995268163076));
#140209=CARTESIAN_POINT('Ctrl Pts',(16.2067351859308,19.6276513592373,9.85411776941796));
#140210=CARTESIAN_POINT('Ctrl Pts',(16.2231231591268,19.7100966739689,9.85828285720516));
#140211=CARTESIAN_POINT('Ctrl Pts',(16.2395131466373,19.7925521223991,9.86244845694073));
#140212=CARTESIAN_POINT('Ctrl Pts',(16.2599662961795,19.8741854840192,9.8666140566763));
#140213=CARTESIAN_POINT('Ctrl Pts',(16.2843678510517,19.9545740278134,9.87077965641186));
#140214=CARTESIAN_POINT('Ctrl Pts',(16.3087969918046,20.035053450603,9.87494996534479));
#140215=CARTESIAN_POINT('Ctrl Pts',(16.3371833165997,20.1142848040861,9.87912027427772));
#140216=CARTESIAN_POINT('Ctrl Pts',(16.3693624790257,20.191861557204,9.88329058321065));
#140217=CARTESIAN_POINT('Ctrl Pts',(16.4015603628986,20.2694834435371,9.88746331837879));
#140218=CARTESIAN_POINT('Ctrl Pts',(16.437555280145,20.3454483968708,9.89163605354694));
#140219=CARTESIAN_POINT('Ctrl Pts',(16.4771361744286,20.4193731513184,9.89580878871509));
#140220=CARTESIAN_POINT('Ctrl Pts',(16.5167895617082,20.4934333000524,9.8999891663097));
#140221=CARTESIAN_POINT('Ctrl Pts',(16.5600418069655,20.5654453913553,9.90416954390431));
#140222=CARTESIAN_POINT('Ctrl Pts',(16.6066377495773,20.6350540212634,9.90834992149893));
#140223=CARTESIAN_POINT('Ctrl Pts',(16.6436006876733,20.6902721225405,9.91166606942054));
#140224=CARTESIAN_POINT('Ctrl Pts',(16.6826668124624,20.7439783287842,9.91498221734214));
#140225=CARTESIAN_POINT('Ctrl Pts',(16.7236914224215,20.7960108589263,9.91829836526375));
#140226=CARTESIAN_POINT('Ctrl Pts',(16.7754602209958,20.8616705099242,9.9224829996568));
#140227=CARTESIAN_POINT('Ctrl Pts',(16.8305455538229,20.924913415419,9.92666763404985));
#140228=CARTESIAN_POINT('Ctrl Pts',(16.8886933634204,20.9853853631597,9.93085226844291));
#140229=CARTESIAN_POINT('Ctrl Pts',(16.9467584068082,21.0457712365676,9.93503094652685));
#140230=CARTESIAN_POINT('Ctrl Pts',(17.0078769523777,21.1033936577097,9.9392096246108));
#140231=CARTESIAN_POINT('Ctrl Pts',(17.07175395795,21.157930429083,9.94338830269474));
#140232=CARTESIAN_POINT('Ctrl Pts',(17.1367759129396,21.2134447328882,9.94764188058018));
#140233=CARTESIAN_POINT('Ctrl Pts',(17.2046558928942,21.2657612997092,9.95189545846561));
#140234=CARTESIAN_POINT('Ctrl Pts',(17.2750424589418,21.314578592159,9.95614903635105));
#140235=CARTESIAN_POINT('Ctrl Pts',(17.3440644440585,21.3624494661354,9.960320150329));
#140236=CARTESIAN_POINT('Ctrl Pts',(17.4154962970282,21.406955261226,9.96449126430695));
#140237=CARTESIAN_POINT('Ctrl Pts',(17.4889737195064,21.4478526015096,9.9686623782849));
#140238=CARTESIAN_POINT('Ctrl Pts',(17.5624264859258,21.4887362182957,9.97283209260527));
#140239=CARTESIAN_POINT('Ctrl Pts',(17.6379230570028,21.5260135615005,9.97700180692565));
#140240=CARTESIAN_POINT('Ctrl Pts',(17.7150725574697,21.5594860797668,9.98117152124603));
#140241=CARTESIAN_POINT('Ctrl Pts',(17.7922193126263,21.5929574069373,9.98534108719007));
#140242=CARTESIAN_POINT('Ctrl Pts',(17.8710184578639,21.6226239960436,9.98951065313412));
#140243=CARTESIAN_POINT('Ctrl Pts',(17.9510583236145,21.6483350880375,9.99368021907816));
#140244=CARTESIAN_POINT('Ctrl Pts',(18.033912292305,21.6749501503078,9.99799638181708));
#140245=CARTESIAN_POINT('Ctrl Pts',(18.1180953501449,21.6973262283484,10.002312544556));
#140246=CARTESIAN_POINT('Ctrl Pts',(18.2031347548813,21.7153526292288,10.0066287072949));
#140247=CARTESIAN_POINT('Ctrl Pts',(18.2854040099531,21.7327918219965,10.0108042714866));
#140248=CARTESIAN_POINT('Ctrl Pts',(18.3684742051326,21.7461603390116,10.0149798356783));
#140249=CARTESIAN_POINT('Ctrl Pts',(18.4519097174452,21.7554105550182,10.01915539987));
#140250=CARTESIAN_POINT('Ctrl Pts',(18.5395593591354,21.765127977445,10.0235418618825));
#140251=CARTESIAN_POINT('Ctrl Pts',(18.6276116092813,21.7703001003685,10.027928323895));
#140252=CARTESIAN_POINT('Ctrl Pts',(18.7155609817199,21.7709335933975,10.0323147859076));
#140253=CARTESIAN_POINT('Ctrl Pts',(18.8035103541584,21.7715670864265,10.0367012479201));
#140254=CARTESIAN_POINT('Ctrl Pts',(18.891356272623,21.767662051318,10.0410877099327));
#140255=CARTESIAN_POINT('Ctrl Pts',(18.9786013944248,21.7592876913421,10.0454741719452));
#140256=CARTESIAN_POINT('Ctrl Pts',(19.0618322388442,21.7512986480824,10.0496588063382));
#140257=CARTESIAN_POINT('Ctrl Pts',(19.1448261598418,21.7392127858656,10.0538434407313));
#140258=CARTESIAN_POINT('Ctrl Pts',(19.2271478044731,21.7230519984553,10.0580280751243));
#140259=CARTESIAN_POINT('Ctrl Pts',(19.3093522744327,21.7069142139256,10.0622067532083));
#140260=CARTESIAN_POINT('Ctrl Pts',(19.3908859211793,21.6867131129897,10.0663854312922));
#140261=CARTESIAN_POINT('Ctrl Pts',(19.4713181268662,21.6625223800313,10.0705641093762));
#140262=CARTESIAN_POINT('Ctrl Pts',(19.5531920220343,21.6378980455703,10.0748176872616));
#140263=CARTESIAN_POINT('Ctrl Pts',(19.6339241211584,21.6091396900263,10.079071265147));
#140264=CARTESIAN_POINT('Ctrl Pts',(19.7130706518194,21.5763796014057,10.0833248430325));
#140265=CARTESIAN_POINT('Ctrl Pts',(19.7906827725417,21.544254631029,10.0874959570104));
#140266=CARTESIAN_POINT('Ctrl Pts',(19.8667698102182,21.5082818897807,10.0916670709884));
#140267=CARTESIAN_POINT('Ctrl Pts',(19.9409299364302,21.4686359601469,10.0958381849663));
#140268=CARTESIAN_POINT('Ctrl Pts',(20.0150651774957,21.4290033340877,10.1000078992867));
#140269=CARTESIAN_POINT('Ctrl Pts',(20.0872743858818,21.3857001842594,10.1041776136071));
#140270=CARTESIAN_POINT('Ctrl Pts',(20.1571790379496,21.3389477028209,10.1083473279274));
#140271=CARTESIAN_POINT('Ctrl Pts',(20.22708120251,21.2921968850363,10.1125168938715));
#140272=CARTESIAN_POINT('Ctrl Pts',(20.2946785918821,21.2419972361384,10.1166864598155));
#140273=CARTESIAN_POINT('Ctrl Pts',(20.3596216126351,21.1886133020724,10.1208560257596));
#140274=CARTESIAN_POINT('Ctrl Pts',(20.4268479498819,21.1333524547408,10.1251721884985));
#140275=CARTESIAN_POINT('Ctrl Pts',(20.4912293829738,21.0746795720027,10.1294883512374));
#140276=CARTESIAN_POINT('Ctrl Pts',(20.5524169502583,21.0129322392957,10.1338045139763));
#140277=CARTESIAN_POINT('Ctrl Pts',(20.6116113389744,20.9531963194569,10.137980078168));
#140278=CARTESIAN_POINT('Ctrl Pts',(20.6678164672702,20.8905835561607,10.1421556423597));
#140279=CARTESIAN_POINT('Ctrl Pts',(20.7207564953884,20.8254344607422,10.1463312065514));
#140280=CARTESIAN_POINT('Ctrl Pts',(20.7763703984739,20.7569948393913,10.1507176685639));
#140281=CARTESIAN_POINT('Ctrl Pts',(20.8283803483074,20.6857564036306,10.1551041305764));
#140282=CARTESIAN_POINT('Ctrl Pts',(20.8765183429016,20.6121477974611,10.159490592589));
#140283=CARTESIAN_POINT('Ctrl Pts',(20.9246563374958,20.5385391912916,10.1638770546015));
#140284=CARTESIAN_POINT('Ctrl Pts',(20.9689221504901,20.4625609543414,10.1682635166141));
#140285=CARTESIAN_POINT('Ctrl Pts',(21.0091047687182,20.3846687315233,10.1726499786266));
#140286=CARTESIAN_POINT('Ctrl Pts',(21.0474385251168,20.3103604453409,10.1768346130197));
#140287=CARTESIAN_POINT('Ctrl Pts',(21.0821992629535,20.2340338438631,10.1810192474127));
#140288=CARTESIAN_POINT('Ctrl Pts',(21.113169743127,20.1560668406992,10.1852038818058));
#140289=CARTESIAN_POINT('Ctrl Pts',(21.1440961406553,20.0782108139138,10.1893825598897));
#140290=CARTESIAN_POINT('Ctrl Pts',(21.1712428282378,19.9987194471869,10.1935612379736));
#140291=CARTESIAN_POINT('Ctrl Pts',(21.1944386775071,19.9179947059399,10.1977399160576));
#140292=CARTESIAN_POINT('Ctrl Pts',(21.218050295704,19.835823031722,10.201993493943));
#140293=CARTESIAN_POINT('Ctrl Pts',(21.2375678238504,19.7523737600797,10.2062470718285));
#140294=CARTESIAN_POINT('Ctrl Pts',(21.252862289631,19.6680916383777,10.2105006497139));
#140295=CARTESIAN_POINT('Ctrl Pts',(21.2678602423477,19.585443490068,10.2146717636918));
#140296=CARTESIAN_POINT('Ctrl Pts',(21.2787973301571,19.5019949698559,10.2188428776698));
#140297=CARTESIAN_POINT('Ctrl Pts',(21.2856028472,19.4181784500398,10.2230139916477));
#140298=CARTESIAN_POINT('Ctrl Pts',(21.2924060805859,19.3343900556663,10.2271837059681));
#140299=CARTESIAN_POINT('Ctrl Pts',(21.2950804593957,19.2502343650758,10.2313534202885));
#140300=CARTESIAN_POINT('Ctrl Pts',(21.2936070835643,19.1661493838661,10.2355231346089));
#140301=CARTESIAN_POINT('Ctrl Pts',(21.2921337601619,19.0820673947608,10.2396927005529));
#140302=CARTESIAN_POINT('Ctrl Pts',(21.2865129844866,18.9980565699809,10.243862266497));
#140303=CARTESIAN_POINT('Ctrl Pts',(21.2767779695196,18.9145540559798,10.248031832441));
#140304=CARTESIAN_POINT('Ctrl Pts',(21.2667006834357,18.8281156965981,10.2523479951799));
#140305=CARTESIAN_POINT('Ctrl Pts',(21.2522145228802,18.7422225813438,10.2566641579188));
#140306=CARTESIAN_POINT('Ctrl Pts',(21.2334144574579,18.6573508603364,10.2609803206578));
#140307=CARTESIAN_POINT('Ctrl Pts',(21.2152268021894,18.575243826714,10.2651558848494));
#140308=CARTESIAN_POINT('Ctrl Pts',(21.1930021468739,18.4940931072444,10.2693314490411));
#140309=CARTESIAN_POINT('Ctrl Pts',(21.1668775008281,18.4143149518383,10.2735070132328));
#140310=CARTESIAN_POINT('Ctrl Pts',(21.139433361016,18.3305073914573,10.2778934752453));
#140311=CARTESIAN_POINT('Ctrl Pts',(21.1076851096663,18.2482152402669,10.2822799372579));
#140312=CARTESIAN_POINT('Ctrl Pts',(21.0718481041568,18.1678958623941,10.2866663992704));
#140313=CARTESIAN_POINT('Ctrl Pts',(21.0360110986473,18.0875764845214,10.2910528612829));
#140314=CARTESIAN_POINT('Ctrl Pts',(20.9960856701951,18.0092303623901,10.2954393232955));
#140315=CARTESIAN_POINT('Ctrl Pts',(20.9523407266399,17.9332815566288,10.299825785308));
#140316=CARTESIAN_POINT('Ctrl Pts',(20.9106208944253,17.8608486952342,10.3040091821604));
#140317=CARTESIAN_POINT('Ctrl Pts',(20.8652721209676,17.790326569507,10.3081925790129));
#140318=CARTESIAN_POINT('Ctrl Pts',(20.8164943998508,17.7221020603848,10.3123759758653));
#140319=CARTESIAN_POINT('Ctrl Pts',(20.7677772522461,17.6539622743297,10.3165541776607));
#140320=CARTESIAN_POINT('Ctrl Pts',(20.7156398718341,17.5881148134686,10.3207323794562));
#140321=CARTESIAN_POINT('Ctrl Pts',(20.6603275198124,17.5249210319758,10.3249105812517));
#140322=CARTESIAN_POINT('Ctrl Pts',(20.6050732438256,17.4617936017432,10.3290843960814));
#140323=CARTESIAN_POINT('Ctrl Pts',(20.546650919326,17.4013146604693,10.3332582109111));
#140324=CARTESIAN_POINT('Ctrl Pts',(20.4853475074074,17.3438144419212,10.3374320257408));
#140325=CARTESIAN_POINT('Ctrl Pts',(20.4241713478543,17.2864335811479,10.3415971766513));
#140326=CARTESIAN_POINT('Ctrl Pts',(20.3601263655428,17.2320194202034,10.3457623275617));
#140327=CARTESIAN_POINT('Ctrl Pts',(20.2935357313021,17.1808649545432,10.3499274784722));
#140328=CARTESIAN_POINT('Ctrl Pts',(20.2954164566376,17.1783794293288,9.5499633233039));
#140329=CARTESIAN_POINT('Ctrl Pts',(19.6881794277694,16.7191703127013,9.58795779950289));
#140330=CARTESIAN_POINT('Ctrl Pts',(17.9381456484885,16.3388456091724,9.66834421126236));
#140331=CARTESIAN_POINT('Ctrl Pts',(16.3483940920526,17.7909994706266,9.76278617059814));
#140332=CARTESIAN_POINT('Ctrl Pts',(16.1742904286681,18.9257985710608,9.81923365373494));
#140333=CARTESIAN_POINT('Ctrl Pts',(16.1763511750307,19.2089800092947,9.83328920131125));
#140334=CARTESIAN_POINT('',(16.1740010233873,19.2132890482674,9.76670989018929));
#140335=CARTESIAN_POINT('Ctrl Pts',(20.2935357313021,17.1808649545431,9.48328065833267));
#140336=CARTESIAN_POINT('Ctrl Pts',(20.226846789779,17.129634969907,9.48745093564785));
#140337=CARTESIAN_POINT('Ctrl Pts',(20.1576478303553,17.0817074848001,9.49162121296303));
#140338=CARTESIAN_POINT('Ctrl Pts',(20.0863050570472,17.0373231535749,9.49579149027821));
#140339=CARTESIAN_POINT('Ctrl Pts',(20.0148828973448,16.9928894338572,9.4999664080533));
#140340=CARTESIAN_POINT('Ctrl Pts',(19.9413125544491,16.9520069791659,9.50414132582839));
#140341=CARTESIAN_POINT('Ctrl Pts',(19.8659864662056,16.9148713798379,9.50831624360348));
#140342=CARTESIAN_POINT('Ctrl Pts',(19.7906119470755,16.8777119041871,9.51249384564074));
#140343=CARTESIAN_POINT('Ctrl Pts',(19.713479857659,16.8443042610608,9.516671447678));
#140344=CARTESIAN_POINT('Ctrl Pts',(19.6350021191175,16.8147956720376,9.52084904971526));
#140345=CARTESIAN_POINT('Ctrl Pts',(19.5563968495913,16.7852391298052,9.52503344060388));
#140346=CARTESIAN_POINT('Ctrl Pts',(19.4764420041446,16.7595944266193,9.52921783149249));
#140347=CARTESIAN_POINT('Ctrl Pts',(19.3955636525281,16.7379586469989,9.5334022223811));
#140348=CARTESIAN_POINT('Ctrl Pts',(19.3647456506557,16.7297145188295,9.53499664862326));
#140349=CARTESIAN_POINT('Ctrl Pts',(19.3337936524143,16.7220519237258,9.53659107486542));
#140350=CARTESIAN_POINT('Ctrl Pts',(19.3027314805897,16.7149742583486,9.53818550110757));
#140351=CARTESIAN_POINT('Ctrl Pts',(19.2212075887324,16.6963986471497,9.54237013550062));
#140352=CARTESIAN_POINT('Ctrl Pts',(19.1386209669252,16.6817867038644,9.54655476989367));
#140353=CARTESIAN_POINT('Ctrl Pts',(19.0553917867604,16.6712544774322,9.55073940428672));
#140354=CARTESIAN_POINT('Ctrl Pts',(18.9722810730318,16.6607372423208,9.55491808237066));
#140355=CARTESIAN_POINT('Ctrl Pts',(18.8885300701232,16.654288246849,9.5590967604546));
#140356=CARTESIAN_POINT('Ctrl Pts',(18.804570732492,16.6519728857014,9.56327543853855));
#140357=CARTESIAN_POINT('Ctrl Pts',(18.7191064840744,16.6496160233692,9.56752901642398));
#140358=CARTESIAN_POINT('Ctrl Pts',(18.6334268287623,16.6515425508617,9.57178259430942));
#140359=CARTESIAN_POINT('Ctrl Pts',(18.5479946282975,16.6577663636679,9.57603617219486));
#140360=CARTESIAN_POINT('Ctrl Pts',(18.4642186977459,16.663869515718,9.58020728617281));
#140361=CARTESIAN_POINT('Ctrl Pts',(18.3806811928207,16.6741047825049,9.58437840015076));
#140362=CARTESIAN_POINT('Ctrl Pts',(18.2978184502103,16.6884327252533,9.58854951412871));
#140363=CARTESIAN_POINT('Ctrl Pts',(18.2149835129935,16.7027558601221,9.59271922844909));
#140364=CARTESIAN_POINT('Ctrl Pts',(18.1328233413407,16.7211688651668,9.59688894276946));
#140365=CARTESIAN_POINT('Ctrl Pts',(18.0517667977985,16.7435807292205,9.60105865708984));
#140366=CARTESIAN_POINT('Ctrl Pts',(17.9707131385959,16.7659917957639,9.60522822303388));
#140367=CARTESIAN_POINT('Ctrl Pts',(17.8907634725904,16.7924013149753,9.60939778897792));
#140368=CARTESIAN_POINT('Ctrl Pts',(17.8123328245034,16.8226680260876,9.61356735492197));
#140369=CARTESIAN_POINT('Ctrl Pts',(17.7311446515844,16.8539988774246,9.61788351766089));
#140370=CARTESIAN_POINT('Ctrl Pts',(17.651584793418,16.8894630151456,9.6221996803998));
#140371=CARTESIAN_POINT('Ctrl Pts',(17.5740906315704,16.9288496418883,9.62651584313872));
#140372=CARTESIAN_POINT('Ctrl Pts',(17.499120833894,16.9669532534076,9.6306914073304));
#140373=CARTESIAN_POINT('Ctrl Pts',(17.4260846045835,17.0087274533692,9.63486697152208));
#140374=CARTESIAN_POINT('Ctrl Pts',(17.3553508285749,17.0539356842855,9.63904253571376));
#140375=CARTESIAN_POINT('Ctrl Pts',(17.2810444576937,17.101427275473,9.64342899772631));
#140376=CARTESIAN_POINT('Ctrl Pts',(17.2092797216846,17.152708580808,9.64781545973885));
#140377=CARTESIAN_POINT('Ctrl Pts',(17.1404457653641,17.2074569130478,9.65220192175139));
#140378=CARTESIAN_POINT('Ctrl Pts',(17.0716118090436,17.2622052452876,9.65658838376393));
#140379=CARTESIAN_POINT('Ctrl Pts',(17.0057090169082,17.3204201632973,9.66097484577647));
#140380=CARTESIAN_POINT('Ctrl Pts',(16.9430809195061,17.3817354354488,9.66536130778901));
#140381=CARTESIAN_POINT('Ctrl Pts',(16.8827886985013,17.4407637964061,9.66958416538902));
#140382=CARTESIAN_POINT('Ctrl Pts',(16.8252872091303,17.5029045422553,9.67380702298903));
#140383=CARTESIAN_POINT('Ctrl Pts',(16.7709203169311,17.5678572314245,9.67802988058904));
#140384=CARTESIAN_POINT('Ctrl Pts',(16.7179063153622,17.6311936081462,9.68214765466764));
#140385=CARTESIAN_POINT('Ctrl Pts',(16.6678730797622,17.6972032456021,9.68626542874624));
#140386=CARTESIAN_POINT('Ctrl Pts',(16.6211045875939,17.7655682388182,9.69038320282484));
#140387=CARTESIAN_POINT('Ctrl Pts',(16.57438033231,17.833868567681,9.69449708202705));
#140388=CARTESIAN_POINT('Ctrl Pts',(16.530914960773,17.9045194435154,9.69861096122926));
#140389=CARTESIAN_POINT('Ctrl Pts',(16.4909521572678,17.9771700379653,9.70272484043147));
#140390=CARTESIAN_POINT('Ctrl Pts',(16.451014356568,18.0497751784301,9.70683614577719));
#140391=CARTESIAN_POINT('Ctrl Pts',(16.4145750025456,18.1243771397533,9.7109474511229));
#140392=CARTESIAN_POINT('Ctrl Pts',(16.3818335581791,18.2005975900802,9.71505875646862));
#140393=CARTESIAN_POINT('Ctrl Pts',(16.3475554603697,18.2803952930204,9.71936301761201));
#140394=CARTESIAN_POINT('Ctrl Pts',(16.3173311789841,18.3619666588744,9.7236672787554));
#140395=CARTESIAN_POINT('Ctrl Pts',(16.2913340385439,18.4448518415191,9.72797153989879));
#140396=CARTESIAN_POINT('Ctrl Pts',(16.2665001036005,18.5240284432035,9.73208321292914));
#140397=CARTESIAN_POINT('Ctrl Pts',(16.2455232446819,18.6044033134949,9.73619488595948));
#140398=CARTESIAN_POINT('Ctrl Pts',(16.2285034541843,18.685560128173,9.74030655898983));
#140399=CARTESIAN_POINT('Ctrl Pts',(16.2114791195103,18.7667386112068,9.74441932981085));
#140400=CARTESIAN_POINT('Ctrl Pts',(16.1984140354435,18.84869898642,9.74853210063186));
#140401=CARTESIAN_POINT('Ctrl Pts',(16.1893567554131,18.9310165044539,9.75264487145288));
#140402=CARTESIAN_POINT('Ctrl Pts',(16.1802905487374,19.0134151527258,9.7567616957255));
#140403=CARTESIAN_POINT('Ctrl Pts',(16.1752400549859,19.0961711731434,9.76087851999813));
#140404=CARTESIAN_POINT('Ctrl Pts',(16.1742017924823,19.1788575547115,9.76499534427075));
#140405=CARTESIAN_POINT('Ctrl Pts',(16.1740576564023,19.1903364349233,9.76556685957693));
#140406=CARTESIAN_POINT('Ctrl Pts',(16.1739907628404,19.2018139780891,9.76613837488311));
#140407=CARTESIAN_POINT('Ctrl Pts',(16.1740010233873,19.2132890482674,9.76670989018929));
#140408=CARTESIAN_POINT('Ctrl Pts',(16.174001023388,19.2132890490549,9.76670989022851));
#140409=CARTESIAN_POINT('Ctrl Pts',(16.1741079389015,19.3328599270272,9.77266511192853));
#140410=CARTESIAN_POINT('Ctrl Pts',(16.1825955516607,19.4520702292312,9.77862033362856));
#140411=CARTESIAN_POINT('Ctrl Pts',(16.1992930219785,19.5699714968759,9.78457555532858));
#140412=CARTESIAN_POINT('Ctrl Pts',(16.2067339930653,19.6225123852222,9.78722940837587));
#140413=CARTESIAN_POINT('Ctrl Pts',(16.2158047738395,19.6747937484515,9.78988326142315));
#140414=CARTESIAN_POINT('Ctrl Pts',(16.2264874578014,19.7267333135613,9.79253711447044));
#140415=CARTESIAN_POINT('Ctrl Pts',(16.2433320704913,19.8086323813112,9.79672174886349));
#140416=CARTESIAN_POINT('Ctrl Pts',(16.2642246666771,19.8898577370365,9.80090638325653));
#140417=CARTESIAN_POINT('Ctrl Pts',(16.2890969179465,19.969978866218,9.80509101764958));
#140418=CARTESIAN_POINT('Ctrl Pts',(16.3139337666449,20.0499859528891,9.80926969573353));
#140419=CARTESIAN_POINT('Ctrl Pts',(16.3427388836329,20.1288914993742,9.81344837381748));
#140420=CARTESIAN_POINT('Ctrl Pts',(16.3753929533288,20.2062752380084,9.81762705190142));
#140421=CARTESIAN_POINT('Ctrl Pts',(16.4086323237558,20.2850460245429,9.82188062978686));
#140422=CARTESIAN_POINT('Ctrl Pts',(16.4458598919279,20.3622394375428,9.82613420767229));
#140423=CARTESIAN_POINT('Ctrl Pts',(16.4868966678982,20.4374283977701,9.83038778555773));
#140424=CARTESIAN_POINT('Ctrl Pts',(16.5271378658896,20.5111596732842,9.83455889953568));
#140425=CARTESIAN_POINT('Ctrl Pts',(16.5710416613174,20.5829631005169,9.83873001351363));
#140426=CARTESIAN_POINT('Ctrl Pts',(16.6183914981669,20.6524578269833,9.84290112749158));
#140427=CARTESIAN_POINT('Ctrl Pts',(16.6657254463213,20.7219292338231,9.84707084181195));
#140428=CARTESIAN_POINT('Ctrl Pts',(16.7165028805481,20.7890930986176,9.85124055613233));
#140429=CARTESIAN_POINT('Ctrl Pts',(16.7704633948897,20.8535967248207,9.8554102704527));
#140430=CARTESIAN_POINT('Ctrl Pts',(16.8244219890847,20.9180980557081,9.85957983639674));
#140431=CARTESIAN_POINT('Ctrl Pts',(16.8815631423605,20.9799389839165,9.86374940234079));
#140432=CARTESIAN_POINT('Ctrl Pts',(16.9415864376591,21.0388002137915,9.86791896828483));
#140433=CARTESIAN_POINT('Ctrl Pts',(17.0037200779736,21.0997309318957,9.87223513102375));
#140434=CARTESIAN_POINT('Ctrl Pts',(17.0689419268742,21.1574681514489,9.87655129376267));
#140435=CARTESIAN_POINT('Ctrl Pts',(17.1368790142891,21.2117010163945,9.88086745650159));
#140436=CARTESIAN_POINT('Ctrl Pts',(17.2026030582273,21.2641672514687,9.88504302069327));
#140437=CARTESIAN_POINT('Ctrl Pts',(17.270867749702,21.3133536974898,9.88921858488495));
#140438=CARTESIAN_POINT('Ctrl Pts',(17.3413050297812,21.3590225138316,9.89339414907663));
#140439=CARTESIAN_POINT('Ctrl Pts',(17.4152999294285,21.4069979535195,9.89778061108917));
#140440=CARTESIAN_POINT('Ctrl Pts',(17.4916921547949,21.4510907819032,9.9021670731017));
#140441=CARTESIAN_POINT('Ctrl Pts',(17.5700268579946,21.4910803768047,9.90655353511425));
#140442=CARTESIAN_POINT('Ctrl Pts',(17.6483615611942,21.5310699717063,9.91093999712678));
#140443=CARTESIAN_POINT('Ctrl Pts',(17.7286381814852,21.5669561657755,9.91532645913933));
#140444=CARTESIAN_POINT('Ctrl Pts',(17.8103811197832,21.5985778865007,9.91971292115187));
#140445=CARTESIAN_POINT('Ctrl Pts',(17.8883629443181,21.6287446449807,9.92389755554492));
#140446=CARTESIAN_POINT('Ctrl Pts',(17.9679693803479,21.6551430224068,9.92808218993796));
#140447=CARTESIAN_POINT('Ctrl Pts',(18.0488014484185,21.6775974428168,9.93226682433101));
#140448=CARTESIAN_POINT('Ctrl Pts',(18.1295184620453,21.7000199021387,9.93644550241496));
#140449=CARTESIAN_POINT('Ctrl Pts',(18.2114572030592,21.7185094330108,9.9406241804989));
#140450=CARTESIAN_POINT('Ctrl Pts',(18.2941997096014,21.7329388780391,9.94480285858285));
#140451=CARTESIAN_POINT('Ctrl Pts',(18.3784253161073,21.7476269604994,9.94905643646828));
#140452=CARTESIAN_POINT('Ctrl Pts',(18.4634833368926,21.758107797425,9.95331001435372));
#140453=CARTESIAN_POINT('Ctrl Pts',(18.5489177820416,21.7643007211442,9.95756359223915));
#140454=CARTESIAN_POINT('Ctrl Pts',(18.6326959137597,21.7703735829526,9.96173470621711));
#140455=CARTESIAN_POINT('Ctrl Pts',(18.7168355246874,21.7723232722254,9.96590582019506));
#140456=CARTESIAN_POINT('Ctrl Pts',(18.8008991604928,21.7701257300737,9.97007693417301));
#140457=CARTESIAN_POINT('Ctrl Pts',(18.8849345879332,21.7679289253285,9.97424664849338));
#140458=CARTESIAN_POINT('Ctrl Pts',(18.96889363139,21.7615876649968,9.97841636281375));
#140459=CARTESIAN_POINT('Ctrl Pts',(19.0523387760778,21.7511300013277,9.98258607713412));
#140460=CARTESIAN_POINT('Ctrl Pts',(19.1357809514292,21.7406727097872,9.98675564307817));
#140461=CARTESIAN_POINT('Ctrl Pts',(19.218708808014,21.7260993641991,9.99092520902222));
#140462=CARTESIAN_POINT('Ctrl Pts',(19.3006912586606,21.7074897390852,9.99509477496627));
#140463=CARTESIAN_POINT('Ctrl Pts',(19.3855561111356,21.6882258225098,9.99941093770519));
#140464=CARTESIAN_POINT('Ctrl Pts',(19.4694073254465,21.6646366310369,10.0037271004441));
#140465=CARTESIAN_POINT('Ctrl Pts',(19.5517816392177,21.6368675129855,10.008043263183));
#140466=CARTESIAN_POINT('Ctrl Pts',(19.631472618382,21.6100029710338,10.0122188273747));
#140467=CARTESIAN_POINT('Ctrl Pts',(19.7097810183149,21.5792268589616,10.0163943915664));
#140468=CARTESIAN_POINT('Ctrl Pts',(19.7863076293697,21.5447199174645,10.0205699557581));
#140469=CARTESIAN_POINT('Ctrl Pts',(19.8666994176241,21.5084701123847,10.0249564177706));
#140470=CARTESIAN_POINT('Ctrl Pts',(19.9451241711511,21.4681029519008,10.0293428797831));
#140471=CARTESIAN_POINT('Ctrl Pts',(20.0211501810795,21.423881472503,10.0337293417957));
#140472=CARTESIAN_POINT('Ctrl Pts',(20.0971761910079,21.3796599931052,10.0381158038082));
#140473=CARTESIAN_POINT('Ctrl Pts',(20.1708030131037,21.3315845757053,10.0425022658208));
#140474=CARTESIAN_POINT('Ctrl Pts',(20.2416377781111,21.2799679383722,10.0468887278333));
#140475=CARTESIAN_POINT('Ctrl Pts',(20.3092133305781,21.2307262590371,10.0510733622263));
#140476=CARTESIAN_POINT('Ctrl Pts',(20.3744996423272,21.1780787853436,10.0552579966194));
#140477=CARTESIAN_POINT('Ctrl Pts',(20.4371331217481,21.1222659599345,10.0594426310124));
#140478=CARTESIAN_POINT('Ctrl Pts',(20.4996774501636,21.0665325771742,10.0636213090964));
#140479=CARTESIAN_POINT('Ctrl Pts',(20.559576106015,21.0076430954477,10.0677999871803));
#140480=CARTESIAN_POINT('Ctrl Pts',(20.6164959352301,20.9458801266491,10.0719786652643));
#140481=CARTESIAN_POINT('Ctrl Pts',(20.6744360114764,20.8830101010231,10.0762322431497));
#140482=CARTESIAN_POINT('Ctrl Pts',(20.7292890301006,20.8171628445093,10.0804858210351));
#140483=CARTESIAN_POINT('Ctrl Pts',(20.7807403436638,20.7486781085842,10.0847393989206));
#140484=CARTESIAN_POINT('Ctrl Pts',(20.8311941731145,20.681521082902,10.0889105128985));
#140485=CARTESIAN_POINT('Ctrl Pts',(20.8783767288092,20.6118283153185,10.0930816268765));
#140486=CARTESIAN_POINT('Ctrl Pts',(20.9220309952966,20.539954613078,10.0972527408544));
#140487=CARTESIAN_POINT('Ctrl Pts',(20.9656706131734,20.4681050287524,10.1014224551748));
#140488=CARTESIAN_POINT('Ctrl Pts',(21.0057840545746,20.3940763560658,10.1055921694952));
#140489=CARTESIAN_POINT('Ctrl Pts',(21.0421580885472,20.3182516598651,10.1097618838155));
#140490=CARTESIAN_POINT('Ctrl Pts',(21.0785308281756,20.2424296618325,10.1139314497596));
#140491=CARTESIAN_POINT('Ctrl Pts',(21.111164226736,20.1648121825011,10.1181010157036));
#140492=CARTESIAN_POINT('Ctrl Pts',(21.1398920226671,20.0858048783968,10.1222705816477));
#140493=CARTESIAN_POINT('Ctrl Pts',(21.1696298524636,20.0040197749462,10.1265867443866));
#140494=CARTESIAN_POINT('Ctrl Pts',(21.1951821474478,19.9207457915132,10.1309029071255));
#140495=CARTESIAN_POINT('Ctrl Pts',(21.2164203674167,19.8364511327311,10.1352190698644));
#140496=CARTESIAN_POINT('Ctrl Pts',(21.236966754604,19.7549023635926,10.1393946340561));
#140497=CARTESIAN_POINT('Ctrl Pts',(21.253475766424,19.6723988660725,10.1435701982478));
#140498=CARTESIAN_POINT('Ctrl Pts',(21.2658832925888,19.5893741438177,10.1477457624395));
#140499=CARTESIAN_POINT('Ctrl Pts',(21.278917493404,19.5021560402143,10.152132224452));
#140500=CARTESIAN_POINT('Ctrl Pts',(21.2874249313198,19.4143632551381,10.1565186864645));
#140501=CARTESIAN_POINT('Ctrl Pts',(21.291393102574,19.3265011640939,10.1609051484771));
#140502=CARTESIAN_POINT('Ctrl Pts',(21.2953612738282,19.2386390730496,10.1652916104896));
#140503=CARTESIAN_POINT('Ctrl Pts',(21.294790258252,19.150708255748,10.1696780725022));
#140504=CARTESIAN_POINT('Ctrl Pts',(21.2897303495757,19.0632083214199,10.1740645345147));
#140505=CARTESIAN_POINT('Ctrl Pts',(21.2849027735544,18.9797260667271,10.1782495861007));
#140506=CARTESIAN_POINT('Ctrl Pts',(21.2759715218878,18.8963252255079,10.1824346376866));
#140507=CARTESIAN_POINT('Ctrl Pts',(21.2629419677493,18.8134417982782,10.1866196892726));
#140508=CARTESIAN_POINT('Ctrl Pts',(21.2499348195045,18.7307008991227,10.1907975441564));
#140509=CARTESIAN_POINT('Ctrl Pts',(21.2328434536036,18.6484760952755,10.1949753990401));
#140510=CARTESIAN_POINT('Ctrl Pts',(21.2117251381584,18.5672002331953,10.1991532539239));
#140511=CARTESIAN_POINT('Ctrl Pts',(21.1906274886263,18.486003905863,10.2033270204519));
#140512=CARTESIAN_POINT('Ctrl Pts',(21.1655108283412,18.4057551192369,10.20750078698));
#140513=CARTESIAN_POINT('Ctrl Pts',(21.1364836587692,18.3268776841708,10.211674553508));
#140514=CARTESIAN_POINT('Ctrl Pts',(21.1074761860984,18.248053772789,10.2158454878527));
#140515=CARTESIAN_POINT('Ctrl Pts',(21.0745636328033,18.1705997951948,10.2200164221973));
#140516=CARTESIAN_POINT('Ctrl Pts',(21.0379042545255,18.0949242024042,10.224187356542));
#140517=CARTESIAN_POINT('Ctrl Pts',(21.0012587547907,18.0192772589526,10.2283567118503));
#140518=CARTESIAN_POINT('Ctrl Pts',(20.9608694496223,17.9454077756907,10.2325260671586));
#140519=CARTESIAN_POINT('Ctrl Pts',(20.9169420720105,17.8737027592017,10.2366954224669));
#140520=CARTESIAN_POINT('Ctrl Pts',(20.8729998723135,17.8019735478277,10.2408661846094));
#140521=CARTESIAN_POINT('Ctrl Pts',(20.8255174487893,17.7324106591192,10.245036946752));
#140522=CARTESIAN_POINT('Ctrl Pts',(20.7747452964143,17.6653743547796,10.2492077088945));
#140523=CARTESIAN_POINT('Ctrl Pts',(20.7239654366808,17.5983278741366,10.2533791041707));
#140524=CARTESIAN_POINT('Ctrl Pts',(20.6698951413505,17.5338091011221,10.257550499447));
#140525=CARTESIAN_POINT('Ctrl Pts',(20.6128256045716,17.4721456795907,10.2617218947232));
#140526=CARTESIAN_POINT('Ctrl Pts',(20.5556935666741,17.4104147258338,10.2658978584064));
#140527=CARTESIAN_POINT('Ctrl Pts',(20.4955560493931,17.3515456983365,10.2700738220896));
#140528=CARTESIAN_POINT('Ctrl Pts',(20.4327411706385,17.2958293978922,10.2742497857728));
#140529=CARTESIAN_POINT('Ctrl Pts',(20.3876731334338,17.2558544054841,10.2772459308004));
#140530=CARTESIAN_POINT('Ctrl Pts',(20.3412276435305,17.2175015523797,10.280242075828));
#140531=CARTESIAN_POINT('Ctrl Pts',(20.2935357313021,17.1808649545432,10.2832382208556));
#140532=CARTESIAN_POINT('Origin',(18.734,19.211,-1.76670989022852));
#140533=CARTESIAN_POINT('',(20.2922817525491,17.1824654639373,11.1497835189211));
#140534=CARTESIAN_POINT('',(20.2948050193864,17.1791827951408,11.0834063379994));
#140535=CARTESIAN_POINT('',(20.2935357313021,17.1808649545432,-1.76670989022852));
#140536=CARTESIAN_POINT('',(16.1740004874608,19.2125798097913,10.6332901097715));
#140537=CARTESIAN_POINT('Ctrl Pts',(16.1772048569635,19.2125971087803,10.6332910657481));
#140538=CARTESIAN_POINT('Ctrl Pts',(16.1753928896008,19.5356421709025,10.6493117789495));
#140539=CARTESIAN_POINT('Ctrl Pts',(16.3822354944161,20.7112478477878,10.7077244277114));
#140540=CARTESIAN_POINT('Ctrl Pts',(18.1490152348825,22.181030878927,10.8085290120338));
#140541=CARTESIAN_POINT('Ctrl Pts',(20.9146847933563,21.3105009952899,10.9357048187152));
#140542=CARTESIAN_POINT('Ctrl Pts',(21.5989574420292,18.8090198185379,11.0494563210109));
#140543=CARTESIAN_POINT('Ctrl Pts',(20.7519189128693,17.541844350173,11.1208158877462));
#140544=CARTESIAN_POINT('Ctrl Pts',(20.2922817525494,17.1824654639375,11.1497835189211));
#140545=CARTESIAN_POINT('Ctrl Pts',(20.2935357313021,17.1808649545432,10.3499274784722));
#140546=CARTESIAN_POINT('Ctrl Pts',(20.2268718754302,17.1296542405312,10.3540972092932));
#140547=CARTESIAN_POINT('Ctrl Pts',(20.1576571101332,17.081710698567,10.3582669401141));
#140548=CARTESIAN_POINT('Ctrl Pts',(20.0862488639036,17.0372881952588,10.3624366709351));
#140549=CARTESIAN_POINT('Ctrl Pts',(20.0148436078252,16.9928675520998,10.3666062271526));
#140550=CARTESIAN_POINT('Ctrl Pts',(19.9412454444601,16.9519678967869,10.3707757833701));
#140551=CARTESIAN_POINT('Ctrl Pts',(19.8658394035043,16.9147988840968,10.3749453395876));
#140552=CARTESIAN_POINT('Ctrl Pts',(19.7873866918356,16.8761281118533,10.3792833606211));
#140553=CARTESIAN_POINT('Ctrl Pts',(19.706977385856,16.8414961001808,10.3836213816546));
#140554=CARTESIAN_POINT('Ctrl Pts',(19.6250697784902,16.8110844494313,10.3879594026881));
#140555=CARTESIAN_POINT('Ctrl Pts',(19.5462302936279,16.7818119684493,10.3921349286813));
#140556=CARTESIAN_POINT('Ctrl Pts',(19.4660032236778,16.7564493936647,10.3963104546746));
#140557=CARTESIAN_POINT('Ctrl Pts',(19.3848125373651,16.7351076272971,10.4004859806679));
#140558=CARTESIAN_POINT('Ctrl Pts',(19.3035638000568,16.7137506016573,10.4046644921445));
#140559=CARTESIAN_POINT('Ctrl Pts',(19.2213505247295,16.6964201991012,10.4088430036211));
#140560=CARTESIAN_POINT('Ctrl Pts',(19.1386057357174,16.6831759953223,10.4130215150977));
#140561=CARTESIAN_POINT('Ctrl Pts',(19.0557327160416,16.6699112668306,10.4172065020673));
#140562=CARTESIAN_POINT('Ctrl Pts',(18.9723269953436,16.6607454158577,10.4213914890369));
#140563=CARTESIAN_POINT('Ctrl Pts',(18.8888248773207,16.6556860745962,10.4255764760064));
#140564=CARTESIAN_POINT('Ctrl Pts',(18.8793465361394,16.6551117878144,10.4260515146675));
#140565=CARTESIAN_POINT('Ctrl Pts',(18.8698669499041,16.6545903564495,10.4265265533285));
#140566=CARTESIAN_POINT('Ctrl Pts',(18.8603867536229,16.6541217493771,10.4270015919895));
#140567=CARTESIAN_POINT('Ctrl Pts',(18.7768753288337,16.6499937711024,10.4311862263825));
#140568=CARTESIAN_POINT('Ctrl Pts',(18.693006041295,16.6499538232249,10.4353708607756));
#140569=CARTESIAN_POINT('Ctrl Pts',(18.6092128353627,16.6540431830901,10.4395554951686));
#140570=CARTESIAN_POINT('Ctrl Pts',(18.5255388986874,16.6581267222578,10.4437341732526));
#140571=CARTESIAN_POINT('Ctrl Pts',(18.4419412840711,16.6663278722549,10.4479128513365));
#140572=CARTESIAN_POINT('Ctrl Pts',(18.3588567381408,16.6786359793502,10.4520915294205));
#140573=CARTESIAN_POINT('Ctrl Pts',(18.2742829614365,16.6911647004195,10.4563451073059));
#140574=CARTESIAN_POINT('Ctrl Pts',(18.1902413093997,16.7079490849927,10.4605986851913));
#140575=CARTESIAN_POINT('Ctrl Pts',(18.1071900176366,16.7289223932339,10.4648522630768));
#140576=CARTESIAN_POINT('Ctrl Pts',(18.0257488372256,16.7494890929688,10.4690233770547));
#140577=CARTESIAN_POINT('Ctrl Pts',(17.9452604262029,16.7740836270437,10.4731944910327));
#140578=CARTESIAN_POINT('Ctrl Pts',(17.8661476315623,16.8025913414462,10.4773656050106));
#140579=CARTESIAN_POINT('Ctrl Pts',(17.7870613839839,16.8310894898098,10.481535319331));
#140580=CARTESIAN_POINT('Ctrl Pts',(17.7093502684716,16.8634980548293,10.4857050336514));
#140581=CARTESIAN_POINT('Ctrl Pts',(17.6334208106691,16.8996528932218,10.4898747479717));
#140582=CARTESIAN_POINT('Ctrl Pts',(17.5574940547626,16.9358064450701,10.4940443139158));
#140583=CARTESIAN_POINT('Ctrl Pts',(17.4833492454957,16.975705806696,10.4982138798598));
#140584=CARTESIAN_POINT('Ctrl Pts',(17.4113705501162,17.0191397539304,10.5023834458039));
#140585=CARTESIAN_POINT('Ctrl Pts',(17.3368611726026,17.0641007851681,10.5066996085428));
#140586=CARTESIAN_POINT('Ctrl Pts',(17.2646735157619,17.1128493061262,10.5110157712817));
#140587=CARTESIAN_POINT('Ctrl Pts',(17.1952016813755,17.1651017291668,10.5153319340206));
#140588=CARTESIAN_POINT('Ctrl Pts',(17.1279928846871,17.2156520350228,10.5195074982123));
#140589=CARTESIAN_POINT('Ctrl Pts',(17.063326023611,17.2694811317354,10.523683062404));
#140590=CARTESIAN_POINT('Ctrl Pts',(17.0015232692733,17.3262919649212,10.5278586265956));
#140591=CARTESIAN_POINT('Ctrl Pts',(16.936599004736,17.3859721782365,10.5322450886082));
#140592=CARTESIAN_POINT('Ctrl Pts',(16.8748361916359,17.4489428422736,10.5366315506207));
#140593=CARTESIAN_POINT('Ctrl Pts',(16.8165619874413,17.5148185627726,10.5410180126333));
#140594=CARTESIAN_POINT('Ctrl Pts',(16.7582877832466,17.5806942832716,10.5454044746458));
#140595=CARTESIAN_POINT('Ctrl Pts',(16.7035024899566,17.6494745589998,10.5497909366583));
#140596=CARTESIAN_POINT('Ctrl Pts',(16.6524807786037,17.7207390393097,10.5541773986709));
#140597=CARTESIAN_POINT('Ctrl Pts',(16.6033728384837,17.789330463214,10.5583993290636));
#140598=CARTESIAN_POINT('Ctrl Pts',(16.5575691753499,17.8604769154311,10.5626212594564));
#140599=CARTESIAN_POINT('Ctrl Pts',(16.5153433201941,17.9338302629828,10.5668431898491));
#140600=CARTESIAN_POINT('Ctrl Pts',(16.4731798646834,18.0070752119517,10.5710588812454));
#140601=CARTESIAN_POINT('Ctrl Pts',(16.4345839361663,18.082520192057,10.5752745726418));
#140602=CARTESIAN_POINT('Ctrl Pts',(16.3997870211447,18.1597865253224,10.5794902640381));
#140603=CARTESIAN_POINT('Ctrl Pts',(16.3650317212893,18.2369604523703,10.5837009137031));
#140604=CARTESIAN_POINT('Ctrl Pts',(16.3340665899183,18.3159509969196,10.587911563368));
#140605=CARTESIAN_POINT('Ctrl Pts',(16.3070776023613,18.3963542635971,10.592122213033));
#140606=CARTESIAN_POINT('Ctrl Pts',(16.2801155537106,18.4766772762055,10.5963286598617));
#140607=CARTESIAN_POINT('Ctrl Pts',(16.2571218975382,18.5584097818784,10.6005351066903));
#140608=CARTESIAN_POINT('Ctrl Pts',(16.238234292144,18.6411284956326,10.604741553519));
#140609=CARTESIAN_POINT('Ctrl Pts',(16.2193575415099,18.7237996707085,10.6089455828908));
#140610=CARTESIAN_POINT('Ctrl Pts',(16.2045822501751,18.807455489948,10.6131496122625));
#140611=CARTESIAN_POINT('Ctrl Pts',(16.19399578679,18.8916591211959,10.6173536416343));
#140612=CARTESIAN_POINT('Ctrl Pts',(16.1834116610726,18.975844158877,10.6215567426863));
#140613=CARTESIAN_POINT('Ctrl Pts',(16.1770145819501,19.0605763228053,10.6257598437382));
#140614=CARTESIAN_POINT('Ctrl Pts',(16.1748403468596,19.145411359684,10.6299629447902));
#140615=CARTESIAN_POINT('Ctrl Pts',(16.1742666403856,19.1677964320708,10.631071999784));
#140616=CARTESIAN_POINT('Ctrl Pts',(16.1739866695752,19.1901886456578,10.6321810547777));
#140617=CARTESIAN_POINT('Ctrl Pts',(16.1740004874608,19.2125798097913,10.6332901097715));
#140618=CARTESIAN_POINT('',(16.1739802642219,19.2096989559289,10.5667098967469));
#140619=CARTESIAN_POINT('Ctrl Pts',(20.2935357313021,17.1808649545432,10.2832382208556));
#140620=CARTESIAN_POINT('Ctrl Pts',(20.2269313029742,17.1296998923603,10.2874225053061));
#140621=CARTESIAN_POINT('Ctrl Pts',(20.1578950951659,17.0818841390033,10.2916067897566));
#140622=CARTESIAN_POINT('Ctrl Pts',(20.0868063265307,17.0376350874972,10.2957910742071));
#140623=CARTESIAN_POINT('Ctrl Pts',(20.055946276678,17.0184263156809,10.2976074965368));
#140624=CARTESIAN_POINT('Ctrl Pts',(20.0246997275378,16.9998890870178,10.2994239188665));
#140625=CARTESIAN_POINT('Ctrl Pts',(19.9930989518198,16.9820383965787,10.3012403411962));
#140626=CARTESIAN_POINT('Ctrl Pts',(19.9202977696528,16.9409143628506,10.3054249755892));
#140627=CARTESIAN_POINT('Ctrl Pts',(19.8453442312191,16.9032842410815,10.3096096099823));
#140628=CARTESIAN_POINT('Ctrl Pts',(19.7686077403709,16.8693794450073,10.3137942443753));
#140629=CARTESIAN_POINT('Ctrl Pts',(19.6919804744194,16.8355229082136,10.3179729224593));
#140630=CARTESIAN_POINT('Ctrl Pts',(19.6135757141379,16.8053813489309,10.3221516005432));
#140631=CARTESIAN_POINT('Ctrl Pts',(19.5337886464594,16.7791410153969,10.3263302786272));
#140632=CARTESIAN_POINT('Ctrl Pts',(19.4525714529348,16.752430342743,10.3305838565126));
#140633=CARTESIAN_POINT('Ctrl Pts',(19.3699223286582,16.7297623675601,10.334837434398));
#140634=CARTESIAN_POINT('Ctrl Pts',(19.2862808103369,16.7112828346924,10.3390910122835));
#140635=CARTESIAN_POINT('Ctrl Pts',(19.2042608460612,16.6931615636291,10.3432621262614));
#140636=CARTESIAN_POINT('Ctrl Pts',(19.1212870932384,16.6790678856914,10.3474332402394));
#140637=CARTESIAN_POINT('Ctrl Pts',(19.0377889319358,16.6690888519003,10.3516043542173));
#140638=CARTESIAN_POINT('Ctrl Pts',(18.9543187892476,16.6591131666705,10.3557740685377));
#140639=CARTESIAN_POINT('Ctrl Pts',(18.8703250439618,16.6532494380237,10.3599437828581));
#140640=CARTESIAN_POINT('Ctrl Pts',(18.7862446699247,16.6515331620698,10.3641134971784));
#140641=CARTESIAN_POINT('Ctrl Pts',(18.7021672878281,16.6498169471884,10.3682830631225));
#140642=CARTESIAN_POINT('Ctrl Pts',(18.6180037430637,16.652247900101,10.3724526290665));
#140643=CARTESIAN_POINT('Ctrl Pts',(18.5341921271336,16.6588094087744,10.3766221950106));
#140644=CARTESIAN_POINT('Ctrl Pts',(18.4474337981802,16.6656016119982,10.3809383577495));
#140645=CARTESIAN_POINT('Ctrl Pts',(18.361053131965,16.6768201947949,10.3852545204884));
#140646=CARTESIAN_POINT('Ctrl Pts',(18.2755295374794,16.6923883119869,10.3895706832273));
#140647=CARTESIAN_POINT('Ctrl Pts',(18.1927918650888,16.7074492993989,10.393746247419));
#140648=CARTESIAN_POINT('Ctrl Pts',(18.1108567316689,16.7265806476473,10.3979218116107));
#140649=CARTESIAN_POINT('Ctrl Pts',(18.030145283277,16.749661230601,10.4020973758024));
#140650=CARTESIAN_POINT('Ctrl Pts',(17.9453572914999,16.7739075589308,10.4064838378149));
#140651=CARTESIAN_POINT('Ctrl Pts',(17.8619204024433,16.8025123689437,10.4108702998274));
#140652=CARTESIAN_POINT('Ctrl Pts',(17.7802998178505,16.8352778018952,10.41525676184));
#140653=CARTESIAN_POINT('Ctrl Pts',(17.6986792332576,16.8680432348467,10.4196432238525));
#140654=CARTESIAN_POINT('Ctrl Pts',(17.6188754477656,16.9049689780518,10.4240296858651));
#140655=CARTESIAN_POINT('Ctrl Pts',(17.5413224142637,16.9458023979171,10.4284161478776));
#140656=CARTESIAN_POINT('Ctrl Pts',(17.4673377107945,16.9847570116046,10.4326007822707));
#140657=CARTESIAN_POINT('Ctrl Pts',(17.3951258047347,17.0274126045708,10.4367854166637));
#140658=CARTESIAN_POINT('Ctrl Pts',(17.3250812297131,17.0735838265015,10.4409700510568));
#140659=CARTESIAN_POINT('Ctrl Pts',(17.2551363544742,17.1196893294125,10.4451487291407));
#140660=CARTESIAN_POINT('Ctrl Pts',(17.1873530634461,17.1693002706272,10.4493274072246));
#140661=CARTESIAN_POINT('Ctrl Pts',(17.1221018691139,17.2221851731129,10.4535060853086));
#140662=CARTESIAN_POINT('Ctrl Pts',(17.0556810940185,17.276017999468,10.457759663194));
#140663=CARTESIAN_POINT('Ctrl Pts',(16.9918845107683,17.3332430884428,10.4620132410795));
#140664=CARTESIAN_POINT('Ctrl Pts',(16.9310725805955,17.3935697481445,10.4662668189649));
#140665=CARTESIAN_POINT('Ctrl Pts',(16.8714396083539,17.4527268578301,10.4704379329429));
#140666=CARTESIAN_POINT('Ctrl Pts',(16.8146769368999,17.5148660125131,10.4746090469208));
#140667=CARTESIAN_POINT('Ctrl Pts',(16.7610901776527,17.5796732905743,10.4787801608988));
#140668=CARTESIAN_POINT('Ctrl Pts',(16.7075213999602,17.6444588219275,10.4829498752191));
#140669=CARTESIAN_POINT('Ctrl Pts',(16.6571267108676,17.7119103443124,10.4871195895395));
#140670=CARTESIAN_POINT('Ctrl Pts',(16.610172482641,17.7816796452478,10.4912893038599));
#140671=CARTESIAN_POINT('Ctrl Pts',(16.5632199252474,17.8514464634922,10.4954588698039));
#140672=CARTESIAN_POINT('Ctrl Pts',(16.5197078414472,17.9235305141742,10.499628435748));
#140673=CARTESIAN_POINT('Ctrl Pts',(16.4798593937703,17.9975544398918,10.503798001692));
#140674=CARTESIAN_POINT('Ctrl Pts',(16.4386099238315,18.0741809555191,10.5081141644309));
#140675=CARTESIAN_POINT('Ctrl Pts',(16.4012867603008,18.1528858318599,10.5124303271698));
#140676=CARTESIAN_POINT('Ctrl Pts',(16.3680847835396,18.2332243669834,10.5167464899088));
#140677=CARTESIAN_POINT('Ctrl Pts',(16.3359643576791,18.3109458827753,10.5209220541004));
#140678=CARTESIAN_POINT('Ctrl Pts',(16.3077008602571,18.3901957994176,10.5250976182921));
#140679=CARTESIAN_POINT('Ctrl Pts',(16.2834204017388,18.4705544364466,10.5292731824838));
#140680=CARTESIAN_POINT('Ctrl Pts',(16.2579135949821,18.5549717971974,10.5336596444963));
#140681=CARTESIAN_POINT('Ctrl Pts',(16.236802907853,18.6406122578469,10.5380461065089));
#140682=CARTESIAN_POINT('Ctrl Pts',(16.2201737773398,18.726977560163,10.5424325685214));
#140683=CARTESIAN_POINT('Ctrl Pts',(16.2035446468265,18.8133428624791,10.546819030534));
#140684=CARTESIAN_POINT('Ctrl Pts',(16.1913970777482,18.9004324212999,10.5512054925465));
#140685=CARTESIAN_POINT('Ctrl Pts',(16.1837535357011,18.9877446051473,10.555591954559));
#140686=CARTESIAN_POINT('Ctrl Pts',(16.1772957565522,19.0615118189368,10.5592979331155));
#140687=CARTESIAN_POINT('Ctrl Pts',(16.174038011382,19.1355632322755,10.563003911672));
#140688=CARTESIAN_POINT('Ctrl Pts',(16.1740003306697,19.2096988355574,10.5667098902285));
#140689=CARTESIAN_POINT('Ctrl Pts',(16.1705863812103,19.2097193146384,10.566710999223));
#140690=CARTESIAN_POINT('Ctrl Pts',(16.1754041849044,19.9846332056276,10.6053965865622));
#140691=CARTESIAN_POINT('Ctrl Pts',(16.9631830908079,21.6171665575917,10.6864741094618));
#140692=CARTESIAN_POINT('Ctrl Pts',(19.742230707443,22.0652534613628,10.8099435679219));
#140693=CARTESIAN_POINT('Ctrl Pts',(21.6797116249341,19.9081907944462,10.9371193746034));
#140694=CARTESIAN_POINT('Ctrl Pts',(21.1313727624476,17.9036399101574,11.0282736312959));
#140695=CARTESIAN_POINT('Ctrl Pts',(20.3968579109702,17.2560798667746,11.0770359524279));
#140696=CARTESIAN_POINT('Ctrl Pts',(20.2948050193864,17.1791827951408,11.0834063379994));
#140697=CARTESIAN_POINT('Origin',(18.734,19.211,-1.76670989022852));
#140698=CARTESIAN_POINT('',(20.2935357313021,17.1808649545431,11.9498687317474));
#140699=CARTESIAN_POINT('',(20.2935357313021,17.1808649545431,11.8833305127049));
#140700=CARTESIAN_POINT('',(20.2935357313021,17.1808649545432,-1.76670989022852));
#140701=CARTESIAN_POINT('',(16.1739804710165,19.212301045312,11.4332901033202));
#140702=CARTESIAN_POINT('Ctrl Pts',(16.1740003306697,19.212301164443,11.4332901097715));
#140703=CARTESIAN_POINT('Ctrl Pts',(16.174038011382,19.2864367677247,11.436996088328));
#140704=CARTESIAN_POINT('Ctrl Pts',(16.1772957565522,19.3604881810636,11.4407020668845));
#140705=CARTESIAN_POINT('Ctrl Pts',(16.1837535357011,19.4342553948533,11.444408045441));
#140706=CARTESIAN_POINT('Ctrl Pts',(16.1910453870482,19.5175502156942,11.448592679834));
#140707=CARTESIAN_POINT('Ctrl Pts',(16.2024358975503,19.6006424250678,11.4527773142271));
#140708=CARTESIAN_POINT('Ctrl Pts',(16.217906819526,19.6830965019697,11.4569619486201));
#140709=CARTESIAN_POINT('Ctrl Pts',(16.2333557205591,19.765433215699,11.4611406267041));
#140710=CARTESIAN_POINT('Ctrl Pts',(16.2528734125179,19.8471331528557,11.465319304788));
#140711=CARTESIAN_POINT('Ctrl Pts',(16.2763898192683,19.927765093712,11.4694979828719));
#140712=CARTESIAN_POINT('Ctrl Pts',(16.3003277407088,20.0098423041589,11.4737515607574));
#140713=CARTESIAN_POINT('Ctrl Pts',(16.3284090988417,20.0908123737401,11.4780051386428));
#140714=CARTESIAN_POINT('Ctrl Pts',(16.3605053261111,20.1702304379142,11.4822587165282));
#140715=CARTESIAN_POINT('Ctrl Pts',(16.3919793053844,20.2481088279428,11.4864298305062));
#140716=CARTESIAN_POINT('Ctrl Pts',(16.4273136905277,20.3244944066986,11.4906009444841));
#140717=CARTESIAN_POINT('Ctrl Pts',(16.4663372697809,20.3989838980285,11.4947720584621));
#140718=CARTESIAN_POINT('Ctrl Pts',(16.5053477542952,20.4734483936902,11.4989417727825));
#140719=CARTESIAN_POINT('Ctrl Pts',(16.5480447610381,20.5460176583688,11.5031114871028));
#140720=CARTESIAN_POINT('Ctrl Pts',(16.5942102750742,20.6163113296,11.5072812014232));
#140721=CARTESIAN_POINT('Ctrl Pts',(16.6403741463432,20.6866024994807,11.5114507673673));
#140722=CARTESIAN_POINT('Ctrl Pts',(16.6900060262588,20.7546178528607,11.5156203333113));
#140723=CARTESIAN_POINT('Ctrl Pts',(16.7428443053794,20.8200055934583,11.5197898992554));
#140724=CARTESIAN_POINT('Ctrl Pts',(16.7975403132109,20.8876922863507,11.5241060619943));
#140725=CARTESIAN_POINT('Ctrl Pts',(16.8556720579015,20.9525627446115,11.5284222247332));
#140726=CARTESIAN_POINT('Ctrl Pts',(16.916904887788,21.0142651921377,11.5327383874721));
#140727=CARTESIAN_POINT('Ctrl Pts',(16.9761430646815,21.0739576889257,11.5369139516638));
#140728=CARTESIAN_POINT('Ctrl Pts',(17.0382830139766,21.1306851185866,11.5410895158555));
#140729=CARTESIAN_POINT('Ctrl Pts',(17.1029865459478,21.1841687998498,11.5452650800472));
#140730=CARTESIAN_POINT('Ctrl Pts',(17.1709580995008,21.2403538147083,11.5496515420597));
#140731=CARTESIAN_POINT('Ctrl Pts',(17.2417585461138,21.2929584378007,11.5540380040722));
#140732=CARTESIAN_POINT('Ctrl Pts',(17.3149615008576,21.3417110873959,11.5584244660848));
#140733=CARTESIAN_POINT('Ctrl Pts',(17.3881644556013,21.390463736991,11.5628109280973));
#140734=CARTESIAN_POINT('Ctrl Pts',(17.4637693807619,21.4353641822178,11.5671973901099));
#140735=CARTESIAN_POINT('Ctrl Pts',(17.5413224142637,21.4761976020829,11.5715838521224));
#140736=CARTESIAN_POINT('Ctrl Pts',(17.6153071177329,21.5151522157705,11.5757684865154));
#140737=CARTESIAN_POINT('Ctrl Pts',(17.6913399834856,21.5505508359911,11.5799531209085));
#140738=CARTESIAN_POINT('Ctrl Pts',(17.7690449301557,21.5821730668978,11.5841377553015));
#140739=CARTESIAN_POINT('Ctrl Pts',(17.8466392734521,21.6137502874729,11.5883164333855));
#140740=CARTESIAN_POINT('Ctrl Pts',(17.9259005477805,21.6415616236984,11.5924951114694));
#140741=CARTESIAN_POINT('Ctrl Pts',(18.0064282347094,21.6654325874532,11.5966737895534));
#140742=CARTESIAN_POINT('Ctrl Pts',(18.0883993225523,21.6897314210775,11.6009273674388));
#140743=CARTESIAN_POINT('Ctrl Pts',(18.1716822438311,21.7099470058045,11.6051809453242));
#140744=CARTESIAN_POINT('Ctrl Pts',(18.2558333466883,21.7259466498637,11.6094345232097));
#140745=CARTESIAN_POINT('Ctrl Pts',(18.3383530162092,21.7416361096021,11.6136056371876));
#140746=CARTESIAN_POINT('Ctrl Pts',(18.4217070321714,21.7532715484977,11.6177767511656));
#140747=CARTESIAN_POINT('Ctrl Pts',(18.5054636294713,21.7607786428131,11.6219478651435));
#140748=CARTESIAN_POINT('Ctrl Pts',(18.589192121436,21.7682832180504,11.6261175794639));
#140749=CARTESIAN_POINT('Ctrl Pts',(18.6733224686327,21.7716621589129,11.6302872937843));
#140750=CARTESIAN_POINT('Ctrl Pts',(18.7574168390729,21.7708928984721,11.6344570081046));
#140751=CARTESIAN_POINT('Ctrl Pts',(18.8415082170746,21.7701236654049,11.6386265740487));
#140752=CARTESIAN_POINT('Ctrl Pts',(18.9255631608594,21.7652065295826,11.6427961399927));
#140753=CARTESIAN_POINT('Ctrl Pts',(19.0091442611984,21.75617104249,11.6469657059368));
#140754=CARTESIAN_POINT('Ctrl Pts',(19.095663969917,21.7468178788177,11.6512818686757));
#140755=CARTESIAN_POINT('Ctrl Pts',(19.1816753701872,21.7330514297719,11.6555980314146));
#140756=CARTESIAN_POINT('Ctrl Pts',(19.2667015333779,21.7149626747092,11.6599141941535));
#140757=CARTESIAN_POINT('Ctrl Pts',(19.3489579782457,21.6974631589401,11.6640897583452));
#140758=CARTESIAN_POINT('Ctrl Pts',(19.4302919452563,21.6759187771978,11.6682653225369));
#140759=CARTESIAN_POINT('Ctrl Pts',(19.510286051879,21.6504630486355,11.6724408867286));
#140760=CARTESIAN_POINT('Ctrl Pts',(19.5943204706595,21.6237216117387,11.6768273487411));
#140761=CARTESIAN_POINT('Ctrl Pts',(19.6768755727334,21.5926635253051,11.6812138107537));
#140762=CARTESIAN_POINT('Ctrl Pts',(19.757492206768,21.557500309543,11.6856002727662));
#140763=CARTESIAN_POINT('Ctrl Pts',(19.8381088408025,21.5223370937809,11.6899867347787));
#140764=CARTESIAN_POINT('Ctrl Pts',(19.9167865216175,21.4830690758565,11.6943731967913));
#140765=CARTESIAN_POINT('Ctrl Pts',(19.9930989518204,21.4399616034209,11.6987596588038));
#140766=CARTESIAN_POINT('Ctrl Pts',(20.0659001339874,21.3988375696928,11.7029442931969));
#140767=CARTESIAN_POINT('Ctrl Pts',(20.1368199197944,21.3540665637942,11.7071289275899));
#140768=CARTESIAN_POINT('Ctrl Pts',(20.205469425502,21.3058455145458,11.711313561983));
#140769=CARTESIAN_POINT('Ctrl Pts',(20.2740212171354,21.2576931019925,11.7154922400669));
#140770=CARTESIAN_POINT('Ctrl Pts',(20.3403087741465,21.2061006624661,11.7196709181509));
#140771=CARTESIAN_POINT('Ctrl Pts',(20.4039685866086,21.1513105214735,11.7238495962348));
#140772=CARTESIAN_POINT('Ctrl Pts',(20.4687694554575,21.0955383065805,11.7281031741202));
#140773=CARTESIAN_POINT('Ctrl Pts',(20.5308470287299,21.036452862187,11.7323567520057));
#140774=CARTESIAN_POINT('Ctrl Pts',(20.5898495933098,20.9743554057569,11.7366103298911));
#140775=CARTESIAN_POINT('Ctrl Pts',(20.6477082780412,20.9134618296929,11.740781443869));
#140776=CARTESIAN_POINT('Ctrl Pts',(20.7026097887107,20.8496723357183,11.744952557847));
#140777=CARTESIAN_POINT('Ctrl Pts',(20.7542579245554,20.7833097399276,11.7491236718249));
#140778=CARTESIAN_POINT('Ctrl Pts',(20.8058887293692,20.7169694127468,11.7532933861453));
#140779=CARTESIAN_POINT('Ctrl Pts',(20.8542680451849,20.6480580612728,11.7574631004657));
#140780=CARTESIAN_POINT('Ctrl Pts',(20.8991399066357,20.5769316178687,11.761632814786));
#140781=CARTESIAN_POINT('Ctrl Pts',(20.9440101713531,20.5058077054488,11.7658023807301));
#140782=CARTESIAN_POINT('Ctrl Pts',(20.9853729851228,20.4324692473493,11.7699719466741));
#140783=CARTESIAN_POINT('Ctrl Pts',(21.0230164347473,20.3573000311684,11.7741415126182));
#140784=CARTESIAN_POINT('Ctrl Pts',(21.0619833816224,20.2794879580778,11.7784576753571));
#140785=CARTESIAN_POINT('Ctrl Pts',(21.0969643161937,20.1997144642828,11.782773838096));
#140786=CARTESIAN_POINT('Ctrl Pts',(21.1277775852798,20.1184298166866,11.7870900008349));
#140787=CARTESIAN_POINT('Ctrl Pts',(21.1575871153665,20.0397930079361,11.7912655650266));
#140788=CARTESIAN_POINT('Ctrl Pts',(21.1834962335157,19.9597424478441,11.7954411292183));
#140789=CARTESIAN_POINT('Ctrl Pts',(21.2053912869579,19.8787013604515,11.7996166934099));
#140790=CARTESIAN_POINT('Ctrl Pts',(21.2283922074989,19.7935670803916,11.8040031554225));
#140791=CARTESIAN_POINT('Ctrl Pts',(21.246962782828,19.7073401510526,11.808389617435));
#140792=CARTESIAN_POINT('Ctrl Pts',(21.2610323380592,19.6205211379197,11.8127760794476));
#140793=CARTESIAN_POINT('Ctrl Pts',(21.2751018932903,19.5337021247869,11.8171625414601));
#140794=CARTESIAN_POINT('Ctrl Pts',(21.2846704408994,19.4462916129091,11.8215490034726));
#140795=CARTESIAN_POINT('Ctrl Pts',(21.2897303495757,19.3587916785811,11.8259354654852));
#140796=CARTESIAN_POINT('Ctrl Pts',(21.2945575272397,19.2753163125985,11.830120171733));
#140797=CARTESIAN_POINT('Ctrl Pts',(21.2952996738552,19.1914488528641,11.8343048779808));
#140798=CARTESIAN_POINT('Ctrl Pts',(21.2919118781325,19.1076229052994,11.8384895842286));
#140799=CARTESIAN_POINT('Ctrl Pts',(21.2885289204165,19.0239166669875,11.8426683144263));
#140800=CARTESIAN_POINT('Ctrl Pts',(21.2810277540026,18.9402522788518,11.8468470446241));
#140801=CARTESIAN_POINT('Ctrl Pts',(21.2694153767469,18.8570665777929,11.8510257748218));
#140802=CARTESIAN_POINT('Ctrl Pts',(21.2578166868035,18.7739789263091,11.8551995796212));
#140803=CARTESIAN_POINT('Ctrl Pts',(21.2421164820731,18.6913692935119,11.8593733844205));
#140804=CARTESIAN_POINT('Ctrl Pts',(21.222373696678,18.6096711833937,11.8635471892198));
#140805=CARTESIAN_POINT('Ctrl Pts',(21.2026437041566,18.5280260117835,11.8677182894891));
#140806=CARTESIAN_POINT('Ctrl Pts',(21.1788764395505,18.4472916360316,11.8718893897583));
#140807=CARTESIAN_POINT('Ctrl Pts',(21.1511820426494,18.3678920752992,11.8760604900275));
#140808=CARTESIAN_POINT('Ctrl Pts',(21.1234972832826,18.2885201452817,11.8802301387713));
#140809=CARTESIAN_POINT('Ctrl Pts',(21.091888257503,18.2104825415903,11.884399787515));
#140810=CARTESIAN_POINT('Ctrl Pts',(21.056514760822,18.1341874881094,11.8885694362588));
#140811=CARTESIAN_POINT('Ctrl Pts',(21.0211429628484,18.0578960984727,11.8927388847675));
#140812=CARTESIAN_POINT('Ctrl Pts',(20.9820072479425,17.9833475094823,11.8969083332763));
#140813=CARTESIAN_POINT('Ctrl Pts',(20.9393147224051,17.9109280884722,11.901077781785));
#140814=CARTESIAN_POINT('Ctrl Pts',(20.8965841485715,17.8384441260572,11.9052509461763));
#140815=CARTESIAN_POINT('Ctrl Pts',(20.8502906654426,17.7680935196513,11.9094241105676));
#140816=CARTESIAN_POINT('Ctrl Pts',(20.8006860848068,17.7002357474225,11.9135972749589));
#140817=CARTESIAN_POINT('Ctrl Pts',(20.7510600241068,17.6323485910264,11.9177722464381));
#140818=CARTESIAN_POINT('Ctrl Pts',(20.6981202983251,17.5669567780695,11.9219472179173));
#140819=CARTESIAN_POINT('Ctrl Pts',(20.6421591183025,17.50438675171,11.9261221893965));
#140820=CARTESIAN_POINT('Ctrl Pts',(20.5861048294898,17.4417126206934,11.9303041072365));
#140821=CARTESIAN_POINT('Ctrl Pts',(20.5270193651102,17.3818699857993,11.9344860250764));
#140822=CARTESIAN_POINT('Ctrl Pts',(20.4652317777209,17.3251483271982,11.9386679429164));
#140823=CARTESIAN_POINT('Ctrl Pts',(20.4100681147629,17.2745075012702,11.9424015391934));
#140824=CARTESIAN_POINT('Ctrl Pts',(20.3527513018397,17.2263539471644,11.9461351354704));
#140825=CARTESIAN_POINT('Ctrl Pts',(20.2935357313021,17.1808649545431,11.9498687317474));
#140826=CARTESIAN_POINT('Ctrl Pts',(20.2922817525494,17.1824654639375,11.1497835189211));
#140827=CARTESIAN_POINT('Ctrl Pts',(20.0792747203257,17.0159205528436,11.1632078233067));
#140828=CARTESIAN_POINT('Ctrl Pts',(19.0902279311992,16.4618740896682,11.2190240632529));
#140829=CARTESIAN_POINT('Ctrl Pts',(16.9631832240595,16.8048336241861,11.3135258905591));
#140830=CARTESIAN_POINT('Ctrl Pts',(16.1754043777096,18.4373668536376,11.3946034134798));
#140831=CARTESIAN_POINT('Ctrl Pts',(16.1705865747788,19.2122806865248,11.4332890008399));
#140832=CARTESIAN_POINT('',(16.1740004874608,19.2094201902091,11.3667098902285));
#140833=CARTESIAN_POINT('Ctrl Pts',(20.2948050193864,17.1791827951408,11.0834063379994));
#140834=CARTESIAN_POINT('Ctrl Pts',(19.7177436634564,16.7443658317468,11.1194278879883));
#140835=CARTESIAN_POINT('Ctrl Pts',(18.0373628378674,16.3338524237142,11.1978413735377));
#140836=CARTESIAN_POINT('Ctrl Pts',(16.3822353164858,17.7107520392007,11.2922755723079));
#140837=CARTESIAN_POINT('Ctrl Pts',(16.1753926962513,18.8863578053553,11.3506882210889));
#140838=CARTESIAN_POINT('Ctrl Pts',(16.1772046638934,19.209402892261,11.3667089343096));
#140839=CARTESIAN_POINT('Ctrl Pts',(16.1740004874608,19.2094201902091,11.3667098902285));
#140840=CARTESIAN_POINT('Ctrl Pts',(16.1739481146197,19.2942876523606,11.3709134538372));
#140841=CARTESIAN_POINT('Ctrl Pts',(16.1781202862138,19.3791700299234,11.3751170174459));
#140842=CARTESIAN_POINT('Ctrl Pts',(16.1864949217896,19.463622003183,11.3793205810546));
#140843=CARTESIAN_POINT('Ctrl Pts',(16.1948707822013,19.5480863280015,11.3835247594573));
#140844=CARTESIAN_POINT('Ctrl Pts',(16.2074502833288,19.6321196761629,11.3877289378599));
#140845=CARTESIAN_POINT('Ctrl Pts',(16.2241595327125,19.7152824890538,11.3919331162626));
#140846=CARTESIAN_POINT('Ctrl Pts',(16.2408759290273,19.7984808725962,11.3961390928892));
#140847=CARTESIAN_POINT('Ctrl Pts',(16.2617254950327,19.8808075406061,11.4003450695159));
#140848=CARTESIAN_POINT('Ctrl Pts',(16.2865836343726,19.9618349574034,11.4045510461425));
#140849=CARTESIAN_POINT('Ctrl Pts',(16.3114761780105,20.0429745182097,11.408762843948));
#140850=CARTESIAN_POINT('Ctrl Pts',(16.3403882340966,20.1228108093805,11.4129746417534));
#140851=CARTESIAN_POINT('Ctrl Pts',(16.3731460171587,20.200933569338,11.4171864395589));
#140852=CARTESIAN_POINT('Ctrl Pts',(16.4059305542806,20.27912013401,11.4214016772397));
#140853=CARTESIAN_POINT('Ctrl Pts',(16.4425668768386,20.3555899771936,11.4256169149205));
#140854=CARTESIAN_POINT('Ctrl Pts',(16.4828349986459,20.4299569872143,11.4298321526013));
#140855=CARTESIAN_POINT('Ctrl Pts',(16.5231739006092,20.5044547137505,11.4340547994973));
#140856=CARTESIAN_POINT('Ctrl Pts',(16.5671571084148,20.5768418481604,11.4382774463933));
#140857=CARTESIAN_POINT('Ctrl Pts',(16.6145212917448,20.646761124022,11.4425000932893));
#140858=CARTESIAN_POINT('Ctrl Pts',(16.6269438222718,20.6650993339888,11.4436075959693));
#140859=CARTESIAN_POINT('Ctrl Pts',(16.6395987151329,20.6832679625289,11.4447150986492));
#140860=CARTESIAN_POINT('Ctrl Pts',(16.6524807786036,20.7012609606902,11.4458226013291));
#140861=CARTESIAN_POINT('Ctrl Pts',(16.7011549053849,20.7692464566217,11.4500072357222));
#140862=CARTESIAN_POINT('Ctrl Pts',(16.7532538754925,20.8349713096213,11.4541918701152));
#140863=CARTESIAN_POINT('Ctrl Pts',(16.8085402991528,20.8980699275411,11.4583765045082));
#140864=CARTESIAN_POINT('Ctrl Pts',(16.8637480294321,20.9610787323883,11.4625551825922));
#140865=CARTESIAN_POINT('Ctrl Pts',(16.9221339008884,21.0214683841931,11.4667338606761));
#140866=CARTESIAN_POINT('Ctrl Pts',(16.9834181011141,21.0789033741853,11.4709125387601));
#140867=CARTESIAN_POINT('Ctrl Pts',(17.0458007765846,21.1373678450953,11.4751661166455));
#140868=CARTESIAN_POINT('Ctrl Pts',(17.1111864272472,21.1927702956729,11.479419694531));
#140869=CARTESIAN_POINT('Ctrl Pts',(17.1792379481545,21.2447932446887,11.4836732724164));
#140870=CARTESIAN_POINT('Ctrl Pts',(17.2459701575374,21.2958076273233,11.4878443863943));
#140871=CARTESIAN_POINT('Ctrl Pts',(17.3152654110889,21.3435720832561,11.4920155003723));
#140872=CARTESIAN_POINT('Ctrl Pts',(17.3867710660548,21.3878266351598,11.4961866143502));
#140873=CARTESIAN_POINT('Ctrl Pts',(17.4582527266078,21.4320663370211,11.5003563286706));
#140874=CARTESIAN_POINT('Ctrl Pts',(17.5319429246535,21.4727982320514,11.504526042991));
#140875=CARTESIAN_POINT('Ctrl Pts',(17.607460394208,21.5098058892786,11.5086957573113));
#140876=CARTESIAN_POINT('Ctrl Pts',(17.682975176527,21.5468122296146,11.5128653232554));
#140877=CARTESIAN_POINT('Ctrl Pts',(17.7603166876027,21.5800943939658,11.5170348891994));
#140878=CARTESIAN_POINT('Ctrl Pts',(17.8390806772781,21.6094827299397,11.5212044551435));
#140879=CARTESIAN_POINT('Ctrl Pts',(17.9206139116645,21.639904323552,11.5255206178824));
#140880=CARTESIAN_POINT('Ctrl Pts',(18.0036710203269,21.6661529958307,11.5298367806213));
#140881=CARTESIAN_POINT('Ctrl Pts',(18.0877848913435,21.6880962906888,11.5341529433602));
#140882=CARTESIAN_POINT('Ctrl Pts',(18.169158761859,21.7093247850249,11.5383285075519));
#140883=CARTESIAN_POINT('Ctrl Pts',(18.2515211332004,21.7265240396988,11.5425040717436));
#140884=CARTESIAN_POINT('Ctrl Pts',(18.3344390537287,21.7396263168398,11.5466796359353));
#140885=CARTESIAN_POINT('Ctrl Pts',(18.4215449613043,21.7533903588514,11.5510660979478));
#140886=CARTESIAN_POINT('Ctrl Pts',(18.5092634338793,21.7626326086006,11.5554525599604));
#140887=CARTESIAN_POINT('Ctrl Pts',(18.5970892183626,21.7673363311332,11.5598390219729));
#140888=CARTESIAN_POINT('Ctrl Pts',(18.684915002846,21.7720400536657,11.5642254839854));
#140889=CARTESIAN_POINT('Ctrl Pts',(18.7728475188787,21.7722053239559,11.568611945998));
#140890=CARTESIAN_POINT('Ctrl Pts',(18.8603867536229,21.7678782506229,11.5729984080105));
#140891=CARTESIAN_POINT('Ctrl Pts',(18.9438981784122,21.7637502723483,11.5771830424036));
#140892=CARTESIAN_POINT('Ctrl Pts',(19.0273625629855,21.7555188996868,11.5813676767966));
#140893=CARTESIAN_POINT('Ctrl Pts',(19.1103440076205,21.7431858517747,11.5855523111897));
#140894=CARTESIAN_POINT('Ctrl Pts',(19.1932073384403,21.7308703584299,11.5897309892736));
#140895=CARTESIAN_POINT('Ctrl Pts',(19.2755886435823,21.7144648534412,11.5939096673576));
#140896=CARTESIAN_POINT('Ctrl Pts',(19.357054356117,21.6940230102284,11.5980883454415));
#140897=CARTESIAN_POINT('Ctrl Pts',(19.4399802830004,21.6732147616673,11.602341923327));
#140898=CARTESIAN_POINT('Ctrl Pts',(19.521956988875,21.6482240726706,11.6065955012124));
#140899=CARTESIAN_POINT('Ctrl Pts',(19.602535053755,21.6191625485832,11.6108490790978));
#140900=CARTESIAN_POINT('Ctrl Pts',(19.6815509556122,21.5906644388491,11.6150201930758));
#140901=CARTESIAN_POINT('Ctrl Pts',(19.7592215106217,21.5582520908958,11.6191913070537));
#140902=CARTESIAN_POINT('Ctrl Pts',(19.8351372401591,21.5220813006761,11.6233624210317));
#140903=CARTESIAN_POINT('Ctrl Pts',(19.9110274954402,21.4859226479144,11.627532135352));
#140904=CARTESIAN_POINT('Ctrl Pts',(19.9851636797555,21.446008255323,11.6317018496724));
#140905=CARTESIAN_POINT('Ctrl Pts',(20.0571574368626,21.4025415572777,11.6358715639928));
#140906=CARTESIAN_POINT('Ctrl Pts',(20.129148632123,21.359076405964,11.6400411299368));
#140907=CARTESIAN_POINT('Ctrl Pts',(20.1989971583731,21.3120594390258,11.6442106958809));
#140908=CARTESIAN_POINT('Ctrl Pts',(20.2663415518563,21.2617387372493,11.6483802618249));
#140909=CARTESIAN_POINT('Ctrl Pts',(20.3360536911359,21.2096488216756,11.6526964245639));
#140910=CARTESIAN_POINT('Ctrl Pts',(20.4030819081961,21.1540188458219,11.6570125873028));
#140911=CARTESIAN_POINT('Ctrl Pts',(20.4670619896057,21.0951698809248,11.6613287500417));
#140912=CARTESIAN_POINT('Ctrl Pts',(20.5289579265928,21.0382379148694,11.6655043142334));
#140913=CARTESIAN_POINT('Ctrl Pts',(20.5880009674137,20.9782938250444,11.6696798784251));
#140914=CARTESIAN_POINT('Ctrl Pts',(20.6438998067282,20.9156649900375,11.6738554426167));
#140915=CARTESIAN_POINT('Ctrl Pts',(20.7026219635295,20.8498729214604,11.6782419046293));
#140916=CARTESIAN_POINT('Ctrl Pts',(20.7578735784433,20.7811182222702,11.6826283666418));
#140917=CARTESIAN_POINT('Ctrl Pts',(20.809367096106,20.7098166720452,11.6870148286544));
#140918=CARTESIAN_POINT('Ctrl Pts',(20.8608606137687,20.6385151218202,11.6914012906669));
#140919=CARTESIAN_POINT('Ctrl Pts',(20.9085957830846,20.5646672491326,11.6957877526794));
#140920=CARTESIAN_POINT('Ctrl Pts',(20.9523407266398,20.4887184433713,11.700174214692));
#140921=CARTESIAN_POINT('Ctrl Pts',(20.9940729004966,20.4162641547461,11.704358849085));
#140922=CARTESIAN_POINT('Ctrl Pts',(21.0323293070735,20.3416283299438,11.7085434834781));
#140923=CARTESIAN_POINT('Ctrl Pts',(21.06687544764,20.265178422184,11.7127281178711));
#140924=CARTESIAN_POINT('Ctrl Pts',(21.1013724160514,20.1888373314054,11.7169067959551));
#140925=CARTESIAN_POINT('Ctrl Pts',(21.1321694205716,20.1106877022101,11.721085474039));
#140926=CARTESIAN_POINT('Ctrl Pts',(21.159076910497,20.0311231481762,11.7252641521229));
#140927=CARTESIAN_POINT('Ctrl Pts',(21.1864666978412,19.9501324566933,11.7295177300084));
#140928=CARTESIAN_POINT('Ctrl Pts',(21.209825919336,19.8676760341797,11.7337713078938));
#140929=CARTESIAN_POINT('Ctrl Pts',(21.2290051549001,19.7841921815777,11.7380248857793));
#140930=CARTESIAN_POINT('Ctrl Pts',(21.2478125635576,19.7023268263636,11.7421959997572));
#140931=CARTESIAN_POINT('Ctrl Pts',(21.2626005065823,19.6194739920341,11.7463671137352));
#140932=CARTESIAN_POINT('Ctrl Pts',(21.273278340702,19.5360623147051,11.7505382277131));
#140933=CARTESIAN_POINT('Ctrl Pts',(21.2839525917715,19.4526786269701,11.7547079420335));
#140934=CARTESIAN_POINT('Ctrl Pts',(21.2905194146576,19.3687369245929,11.7588776563539));
#140935=CARTESIAN_POINT('Ctrl Pts',(21.2929396556081,19.284673868884,11.7630473706742));
#140936=CARTESIAN_POINT('Ctrl Pts',(21.295359810436,19.2006138044994,11.7672169366183));
#140937=CARTESIAN_POINT('Ctrl Pts',(21.2936336643145,19.1164328552357,11.7713865025623));
#140938=CARTESIAN_POINT('Ctrl Pts',(21.2877741604491,19.0325692363337,11.7755560685064));
#140939=CARTESIAN_POINT('Ctrl Pts',(21.2817086436563,18.945757076048,11.7798722312453));
#140940=CARTESIAN_POINT('Ctrl Pts',(21.2712137402019,18.859285502122,11.7841883939842));
#140941=CARTESIAN_POINT('Ctrl Pts',(21.2563622783628,18.7736345501841,11.7885045567231));
#140942=CARTESIAN_POINT('Ctrl Pts',(21.241994601331,18.6907736689967,11.7926801209148));
#140943=CARTESIAN_POINT('Ctrl Pts',(21.2235499863026,18.6086812165374,11.7968556851065));
#140944=CARTESIAN_POINT('Ctrl Pts',(21.2011460288054,18.5277793383177,11.8010312492982));
#140945=CARTESIAN_POINT('Ctrl Pts',(21.1776105006754,18.442791298555,11.8054177113107));
#140946=CARTESIAN_POINT('Ctrl Pts',(21.1497053305466,18.3591178195345,11.8098041733232));
#140947=CARTESIAN_POINT('Ctrl Pts',(21.1176244749813,18.27722574341,11.8141906353358));
#140948=CARTESIAN_POINT('Ctrl Pts',(21.085543619416,18.1953336672856,11.8185770973483));
#140949=CARTESIAN_POINT('Ctrl Pts',(21.0492873869465,18.115223491295,11.8229635593609));
#140950=CARTESIAN_POINT('Ctrl Pts',(21.0091047687183,18.0373312684769,11.8273500213734));
#140951=CARTESIAN_POINT('Ctrl Pts',(20.970767809012,17.9630167728245,11.8315350054497));
#140952=CARTESIAN_POINT('Ctrl Pts',(20.9287145340175,17.8904443146227,11.835719989526));
#140953=CARTESIAN_POINT('Ctrl Pts',(20.8831270316874,17.8200100641376,11.8399049736022));
#140954=CARTESIAN_POINT('Ctrl Pts',(20.8376158265713,17.749693695458,11.8440829535083));
#140955=CARTESIAN_POINT('Ctrl Pts',(20.7885824023206,17.6815088023905,11.8482609334144));
#140956=CARTESIAN_POINT('Ctrl Pts',(20.7362550110473,17.6158276360418,11.8524389133204));
#140957=CARTESIAN_POINT('Ctrl Pts',(20.6839782703688,17.5502100461501,11.8566128491272));
#140958=CARTESIAN_POINT('Ctrl Pts',(20.6284141773837,17.4870917295154,11.8607867849339));
#140959=CARTESIAN_POINT('Ctrl Pts',(20.5698341380306,17.4268158677868,11.8649607207407));
#140960=CARTESIAN_POINT('Ctrl Pts',(20.5112960173992,17.366583138277,11.8691316697612));
#140961=CARTESIAN_POINT('Ctrl Pts',(20.4497465580658,17.3091891512985,11.8733026187818));
#140962=CARTESIAN_POINT('Ctrl Pts',(20.3854963550796,17.2549427950188,11.8774735678023));
#140963=CARTESIAN_POINT('Ctrl Pts',(20.3554224720524,17.2295514577532,11.8794258827698));
#140964=CARTESIAN_POINT('Ctrl Pts',(20.3247574130354,17.2048492349798,11.8813781977374));
#140965=CARTESIAN_POINT('Ctrl Pts',(20.2935357313021,17.1808649545431,11.8833305127049));
#140966=CARTESIAN_POINT('Origin',(18.734,19.211,-1.76670989022852));
#140967=CARTESIAN_POINT('',(20.2935357313021,17.1808649545432,12.7499597618547));
#140968=CARTESIAN_POINT('',(20.2929505239234,17.1816081970505,12.6831923935391));
#140969=CARTESIAN_POINT('',(20.2935357313021,17.1808649545432,-1.76670989022852));
#140970=CARTESIAN_POINT('',(16.1740010233873,19.2087109517327,12.2332901098107));
#140971=CARTESIAN_POINT('Ctrl Pts',(16.1740010233873,19.2087109517327,12.2332901098107));
#140972=CARTESIAN_POINT('Ctrl Pts',(16.1739252094451,19.293498859929,12.2375129674107));
#140973=CARTESIAN_POINT('Ctrl Pts',(16.1780663695147,19.3784221563148,12.2417358250107));
#140974=CARTESIAN_POINT('Ctrl Pts',(16.1864353355331,19.4630203967139,12.2459586826108));
#140975=CARTESIAN_POINT('Ctrl Pts',(16.1945865434513,19.5454174151127,12.2500716626647));
#140976=CARTESIAN_POINT('Ctrl Pts',(16.2067481850334,19.6275055813485,12.2541846427187));
#140977=CARTESIAN_POINT('Ctrl Pts',(16.2228775801224,19.7088596111236,12.2582976227727));
#140978=CARTESIAN_POINT('Ctrl Pts',(16.2389992540558,19.7901746966527,12.2624086339395));
#140979=CARTESIAN_POINT('Ctrl Pts',(16.25908482094,19.8707558783837,12.2665196451063));
#140980=CARTESIAN_POINT('Ctrl Pts',(16.2830401055299,19.9501857653521,12.2706306562731));
#140981=CARTESIAN_POINT('Ctrl Pts',(16.3069915898918,20.0296030516901,12.2747410152757));
#140982=CARTESIAN_POINT('Ctrl Pts',(16.3348114354692,20.1078689519365,12.2788513742782));
#140983=CARTESIAN_POINT('Ctrl Pts',(16.366355393672,20.1845805144548,12.2829617332808));
#140984=CARTESIAN_POINT('Ctrl Pts',(16.3994039228381,20.264951034063,12.2872681465249));
#140985=CARTESIAN_POINT('Ctrl Pts',(16.4365404963283,20.3436147061446,12.2915745597691));
#140986=CARTESIAN_POINT('Ctrl Pts',(16.4775431085385,20.4201328698599,12.2958809730133));
#140987=CARTESIAN_POINT('Ctrl Pts',(16.5167281737211,20.4932591677035,12.2999964933322));
#140988=CARTESIAN_POINT('Ctrl Pts',(16.5594435017451,20.5644257408165,12.304112013651));
#140989=CARTESIAN_POINT('Ctrl Pts',(16.6054498638678,20.6332778624347,12.3082275339699));
#140990=CARTESIAN_POINT('Ctrl Pts',(16.6514869443887,20.7021759565399,12.3123458022172));
#140991=CARTESIAN_POINT('Ctrl Pts',(16.7008191449123,20.768756147345,12.3164640704645));
#140992=CARTESIAN_POINT('Ctrl Pts',(16.7531665958489,20.8326963417974,12.3205823387118));
#140993=CARTESIAN_POINT('Ctrl Pts',(16.8055945346489,20.8967348487664,12.3247069390843));
#140994=CARTESIAN_POINT('Ctrl Pts',(16.8610466479906,20.9581249187389,12.3288315394568));
#140995=CARTESIAN_POINT('Ctrl Pts',(16.9192065009781,21.0165815007659,12.3329561398293));
#140996=CARTESIAN_POINT('Ctrl Pts',(16.9271149034352,21.0245302515482,12.3335169906232));
#140997=CARTESIAN_POINT('Ctrl Pts',(16.93507332294,21.0324248251516,12.3340778414171));
#140998=CARTESIAN_POINT('Ctrl Pts',(16.9430809195058,21.040264564551,12.334638692211));
#140999=CARTESIAN_POINT('Ctrl Pts',(17.0028274053093,21.0987586301397,12.338823326604));
#141000=CARTESIAN_POINT('Ctrl Pts',(17.0655538444182,21.1544313597729,12.3430079609971));
#141001=CARTESIAN_POINT('Ctrl Pts',(17.1309629349571,21.2069639696394,12.3471925953901));
#141002=CARTESIAN_POINT('Ctrl Pts',(17.1962789237517,21.259421805838,12.3513712734741));
#141003=CARTESIAN_POINT('Ctrl Pts',(17.2642696237805,21.3087481146435,12.355549951558));
#141004=CARTESIAN_POINT('Ctrl Pts',(17.3346011829193,21.3546611091199,12.3597286296419));
#141005=CARTESIAN_POINT('Ctrl Pts',(17.4061933847094,21.4013970610253,12.3639822075274));
#141006=CARTESIAN_POINT('Ctrl Pts',(17.4802108463241,21.4445957903897,12.3682357854128));
#141007=CARTESIAN_POINT('Ctrl Pts',(17.5562664269212,21.484003218397,12.3724893632982));
#141008=CARTESIAN_POINT('Ctrl Pts',(17.6308475216781,21.522646656515,12.3766604772762));
#141009=CARTESIAN_POINT('Ctrl Pts',(17.7073879875327,21.5576442636058,12.3808315912541));
#141010=CARTESIAN_POINT('Ctrl Pts',(17.7854953736982,21.5888012898231,12.3850027052321));
#141011=CARTESIAN_POINT('Ctrl Pts',(17.863576550176,21.6199478609992,12.3891724195525));
#141012=CARTESIAN_POINT('Ctrl Pts',(17.943223175791,21.6472562404631,12.3933421338728));
#141013=CARTESIAN_POINT('Ctrl Pts',(18.0240221782529,21.6705795357392,12.3975118481932));
#141014=CARTESIAN_POINT('Ctrl Pts',(18.1048183055395,21.6939020010724,12.4016814141373));
#141015=CARTESIAN_POINT('Ctrl Pts',(18.1867662859179,21.713239537401,12.4058509800813));
#141016=CARTESIAN_POINT('Ctrl Pts',(18.2694385404877,21.7284953128727,12.4100205460253));
#141017=CARTESIAN_POINT('Ctrl Pts',(18.3550174495409,21.7442874625899,12.4143367087643));
#141018=CARTESIAN_POINT('Ctrl Pts',(18.4413719926984,21.7557053858609,12.4186528715032));
#141019=CARTESIAN_POINT('Ctrl Pts',(18.5280191484745,21.762699803818,12.4229690342421));
#141020=CARTESIAN_POINT('Ctrl Pts',(18.6118437822648,21.7694663793459,12.4271445984338));
#141021=CARTESIAN_POINT('Ctrl Pts',(18.6959417854331,21.7720932477196,12.4313201626255));
#141022=CARTESIAN_POINT('Ctrl Pts',(18.7798750222012,21.7705889283903,12.4354957268171));
#141023=CARTESIAN_POINT('Ctrl Pts',(18.8680475272262,21.7690086294678,12.4398821888297));
#141024=CARTESIAN_POINT('Ctrl Pts',(18.9560376012523,21.7628688832022,12.4442686508422));
#141025=CARTESIAN_POINT('Ctrl Pts',(19.0433447687653,21.7522409988109,12.4486551128548));
#141026=CARTESIAN_POINT('Ctrl Pts',(19.1306519362784,21.7416131144196,12.4530415748673));
#141027=CARTESIAN_POINT('Ctrl Pts',(19.2172756387742,21.7264972665759,12.4574280368799));
#141028=CARTESIAN_POINT('Ctrl Pts',(19.3027314805894,21.7070257416514,12.4618144988924));
#141029=CARTESIAN_POINT('Ctrl Pts',(19.3842553724468,21.6884501304525,12.4659991332855));
#141030=CARTESIAN_POINT('Ctrl Pts',(19.4650199594565,21.6658417144697,12.4701837676785));
#141031=CARTESIAN_POINT('Ctrl Pts',(19.5445962710157,21.6392779259004,12.4743684020716));
#141032=CARTESIAN_POINT('Ctrl Pts',(19.6240593155452,21.6127519475962,12.4785470801555));
#141033=CARTESIAN_POINT('Ctrl Pts',(19.7023370115734,21.5822819240423,12.4827257582395));
#141034=CARTESIAN_POINT('Ctrl Pts',(19.7790117130577,21.5479960461182,12.4869044363234));
#141035=CARTESIAN_POINT('Ctrl Pts',(19.8570607534608,21.5130956184733,12.4911580142089));
#141036=CARTESIAN_POINT('Ctrl Pts',(19.9334482966289,21.4742412996488,12.4954115920943));
#141037=CARTESIAN_POINT('Ctrl Pts',(20.0077511504913,21.4316210857826,12.4996651699797));
#141038=CARTESIAN_POINT('Ctrl Pts',(20.0806134985415,21.3898271479286,12.5038362839577));
#141039=CARTESIAN_POINT('Ctrl Pts',(20.1514708500759,21.3444122698723,12.5080073979356));
#141040=CARTESIAN_POINT('Ctrl Pts',(20.219947025126,21.2956010262204,12.5121785119136));
#141041=CARTESIAN_POINT('Ctrl Pts',(20.2884002223341,21.2468061616529,12.516348226234));
#141042=CARTESIAN_POINT('Ctrl Pts',(20.354473455646,21.1946174617219,12.5205179405544));
#141043=CARTESIAN_POINT('Ctrl Pts',(20.4178196235401,21.1393027447425,12.5246876548747));
#141044=CARTESIAN_POINT('Ctrl Pts',(20.4811635373055,21.0839899960981,12.5288572208188));
#141045=CARTESIAN_POINT('Ctrl Pts',(20.5417802326388,21.0255517547982,12.5330267867628));
#141046=CARTESIAN_POINT('Ctrl Pts',(20.5993568489268,20.9642951337872,12.5371963527068));
#141047=CARTESIAN_POINT('Ctrl Pts',(20.6589577880152,20.9008848055495,12.5415125154458));
#141048=CARTESIAN_POINT('Ctrl Pts',(20.7153005309282,20.8344546059654,12.5458286781847));
#141049=CARTESIAN_POINT('Ctrl Pts',(20.7680821915678,20.765384005948,12.5501448409236));
#141050=CARTESIAN_POINT('Ctrl Pts',(20.8191444951636,20.6985633734613,12.5543204051153));
#141051=CARTESIAN_POINT('Ctrl Pts',(20.8668739298251,20.6292721356226,12.558495969307));
#141052=CARTESIAN_POINT('Ctrl Pts',(20.9110405044756,20.557883306702,12.5626715334986));
#141053=CARTESIAN_POINT('Ctrl Pts',(20.9574378278157,20.4828887977435,12.5670579955112));
#141054=CARTESIAN_POINT('Ctrl Pts',(20.9999026310488,20.4055797420146,12.5714444575237));
#141055=CARTESIAN_POINT('Ctrl Pts',(21.0382239760383,20.3264155585478,12.5758309195363));
#141056=CARTESIAN_POINT('Ctrl Pts',(21.0765453210277,20.2472513750809,12.5802173815488));
#141057=CARTESIAN_POINT('Ctrl Pts',(21.1107230523384,20.166232628037,12.5846038435613));
#141058=CARTESIAN_POINT('Ctrl Pts',(21.1406062076889,20.0838382216157,12.5889903055739));
#141059=CARTESIAN_POINT('Ctrl Pts',(21.1691143947643,20.0052349039716,12.5931749399669));
#141060=CARTESIAN_POINT('Ctrl Pts',(21.193820633909,19.9250871608006,12.59735957436));
#141061=CARTESIAN_POINT('Ctrl Pts',(21.2145578396958,19.8437976010731,12.601544208753));
#141062=CARTESIAN_POINT('Ctrl Pts',(21.2352655286368,19.7626237469725,12.605722886837));
#141063=CARTESIAN_POINT('Ctrl Pts',(21.2520152930198,19.6803117464873,12.6099015649209));
#141064=CARTESIAN_POINT('Ctrl Pts',(21.2646888572062,19.5972821611367,12.6140802430048));
#141065=CARTESIAN_POINT('Ctrl Pts',(21.2775895859223,19.5127643301408,12.6183338208903));
#141066=CARTESIAN_POINT('Ctrl Pts',(21.2862663809328,19.4275033890779,12.6225873987757));
#141067=CARTESIAN_POINT('Ctrl Pts',(21.290648251397,19.3419569342516,12.6268409766611));
#141068=CARTESIAN_POINT('Ctrl Pts',(21.2949451707517,19.2580689643825,12.6310120906391));
#141069=CARTESIAN_POINT('Ctrl Pts',(21.2951121858363,19.1739069330306,12.635183204617));
#141070=CARTESIAN_POINT('Ctrl Pts',(21.2911345092732,19.089908705993,12.639354318595));
#141071=CARTESIAN_POINT('Ctrl Pts',(21.2871581674578,19.0059386653716,12.6435240329154));
#141072=CARTESIAN_POINT('Ctrl Pts',(21.2790399178705,18.9221327790365,12.6476937472357));
#141073=CARTESIAN_POINT('Ctrl Pts',(21.2668170738605,18.8389278694117,12.6518634615561));
#141074=CARTESIAN_POINT('Ctrl Pts',(21.2545946647919,18.7557259205747,12.6560330275001));
#141075=CARTESIAN_POINT('Ctrl Pts',(21.2382680194082,18.6731253609526,12.6602025934442));
#141076=CARTESIAN_POINT('Ctrl Pts',(21.2179260255782,18.5915554912218,12.6643721593882));
#141077=CARTESIAN_POINT('Ctrl Pts',(21.1968688323396,18.5071177254984,12.6686883221271));
#141078=CARTESIAN_POINT('Ctrl Pts',(21.1715088054105,18.4237849880543,12.6730044848661));
#141079=CARTESIAN_POINT('Ctrl Pts',(21.1420010732761,18.3420173585733,12.677320647605));
#141080=CARTESIAN_POINT('Ctrl Pts',(21.1134545524124,18.2629133010223,12.6814962117967));
#141081=CARTESIAN_POINT('Ctrl Pts',(21.0810266246881,18.1852743669888,12.6856717759884));
#141082=CARTESIAN_POINT('Ctrl Pts',(21.044906446266,18.1094958481211,12.68984734018));
#141083=CARTESIAN_POINT('Ctrl Pts',(21.0069619234992,18.0298899364116,12.6942338021926));
#141084=CARTESIAN_POINT('Ctrl Pts',(20.9649426346359,17.9523378315094,12.6986202642051));
#141085=CARTESIAN_POINT('Ctrl Pts',(20.9191207015648,17.8772655738143,12.7030067262177));
#141086=CARTESIAN_POINT('Ctrl Pts',(20.8732987684937,17.8021933161192,12.7073931882302));
#141087=CARTESIAN_POINT('Ctrl Pts',(20.8236745814509,17.7296013416972,12.7117796502428));
#141088=CARTESIAN_POINT('Ctrl Pts',(20.7705691100603,17.6598758076968,12.7161661122553));
#141089=CARTESIAN_POINT('Ctrl Pts',(20.7199091712294,17.5933611681518,12.7203505755775));
#141090=CARTESIAN_POINT('Ctrl Pts',(20.6658929673671,17.5292072036879,12.7245350388997));
#141091=CARTESIAN_POINT('Ctrl Pts',(20.6087685574014,17.4677722879156,12.7287195022218));
#141092=CARTESIAN_POINT('Ctrl Pts',(20.5517322346267,17.4064321062362,12.7328975130026));
#141093=CARTESIAN_POINT('Ctrl Pts',(20.491597541221,17.3478029746891,12.7370755237833));
#141094=CARTESIAN_POINT('Ctrl Pts',(20.4286539389136,17.2922118336501,12.7412535345641));
#141095=CARTESIAN_POINT('Ctrl Pts',(20.3849328686936,17.2535978348975,12.7441556103276));
#141096=CARTESIAN_POINT('Ctrl Pts',(20.3398574537499,17.2164489820464,12.7470576860912));
#141097=CARTESIAN_POINT('Ctrl Pts',(20.2935357313021,17.1808649545432,12.7499597618547));
#141098=CARTESIAN_POINT('Ctrl Pts',(20.2935357313021,17.1808649545431,11.9498687317474));
#141099=CARTESIAN_POINT('Ctrl Pts',(20.2763932885852,17.1676962483536,11.9509495785538));
#141100=CARTESIAN_POINT('Ctrl Pts',(20.2590918286248,17.1547506666131,11.9520304253602));
#141101=CARTESIAN_POINT('Ctrl Pts',(20.2416377781113,17.1420320616279,11.9531112721667));
#141102=CARTESIAN_POINT('Ctrl Pts',(20.1740622256442,17.0927903822927,11.9572959065597));
#141103=CARTESIAN_POINT('Ctrl Pts',(20.1039459219086,17.0467712239067,11.9614805409528));
#141104=CARTESIAN_POINT('Ctrl Pts',(20.0316291334108,17.0042470387188,11.9656651753458));
#141105=CARTESIAN_POINT('Ctrl Pts',(19.9594152789104,16.961783381445,11.9698438534298));
#141106=CARTESIAN_POINT('Ctrl Pts',(19.8850075541816,16.9228050473158,11.9740225315137));
#141107=CARTESIAN_POINT('Ctrl Pts',(19.80877704316,16.887542596152,11.9782012095977));
#141108=CARTESIAN_POINT('Ctrl Pts',(19.7311801550142,16.8516480908937,11.9824547874831));
#141109=CARTESIAN_POINT('Ctrl Pts',(19.6516948805983,16.8196042772377,11.9867083653685));
#141110=CARTESIAN_POINT('Ctrl Pts',(19.5707410268099,16.7916065937816,11.990961943254));
#141111=CARTESIAN_POINT('Ctrl Pts',(19.4913566214456,16.7641517000523,11.9951330572319));
#141112=CARTESIAN_POINT('Ctrl Pts',(19.4105605259053,16.7405876095593,11.9993041712099));
#141113=CARTESIAN_POINT('Ctrl Pts',(19.3287692237664,16.721050287564,12.0034752851878));
#141114=CARTESIAN_POINT('Ctrl Pts',(19.2470053674889,16.7015195215057,12.0076449995082));
#141115=CARTESIAN_POINT('Ctrl Pts',(19.1642474149177,16.68601294719,12.0118147138286));
#141116=CARTESIAN_POINT('Ctrl Pts',(19.0809253355089,16.6746161939521,12.015984428149));
#141117=CARTESIAN_POINT('Ctrl Pts',(18.9976062210572,16.6632198462596,12.020153994093));
#141118=CARTESIAN_POINT('Ctrl Pts',(18.9137234755848,16.6559330903703,12.024323560037));
#141119=CARTESIAN_POINT('Ctrl Pts',(18.8297141852422,16.6527899236491,12.0284931259811));
#141120=CARTESIAN_POINT('Ctrl Pts',(18.742751231888,16.6495362470634,12.03280928872));
#141121=CARTESIAN_POINT('Ctrl Pts',(18.655653196516,16.6507229779044,12.0371254514589));
#141122=CARTESIAN_POINT('Ctrl Pts',(18.5689051504087,16.6563290445464,12.0414416141978));
#141123=CARTESIAN_POINT('Ctrl Pts',(18.484982912779,16.6617524941571,12.0456171783895));
#141124=CARTESIAN_POINT('Ctrl Pts',(18.4013886754037,16.6713116809417,12.0497927425812));
#141125=CARTESIAN_POINT('Ctrl Pts',(18.3185547392491,16.6849348315375,12.0539683067729));
#141126=CARTESIAN_POINT('Ctrl Pts',(18.2315370578984,16.6992460550839,12.0583547687854));
#141127=CARTESIAN_POINT('Ctrl Pts',(18.1453590723574,16.7180424488713,12.062741230798));
#141128=CARTESIAN_POINT('Ctrl Pts',(18.0605056905574,16.7411810966898,12.0671276928105));
#141129=CARTESIAN_POINT('Ctrl Pts',(17.9756523087575,16.7643197445083,12.071514154823));
#141130=CARTESIAN_POINT('Ctrl Pts',(17.8921240580815,16.7918003927741,12.0759006168356));
#141131=CARTESIAN_POINT('Ctrl Pts',(17.8103811197834,16.8234221134992,12.0802870788481));
#141132=CARTESIAN_POINT('Ctrl Pts',(17.7323992952485,16.8535888719792,12.0844717132412));
#141133=CARTESIAN_POINT('Ctrl Pts',(17.6557518403844,16.8876362896632,12.0886563476342));
#141134=CARTESIAN_POINT('Ctrl Pts',(17.5808520242221,16.9254257295027,12.0928409820273));
#141135=CARTESIAN_POINT('Ctrl Pts',(17.5060588186774,16.963161380752,12.0970196601112));
#141136=CARTESIAN_POINT('Ctrl Pts',(17.4330087179883,17.0046282689895,12.1011983381951));
#141137=CARTESIAN_POINT('Ctrl Pts',(17.3620964471734,17.0496391690091,12.1053770162791));
#141138=CARTESIAN_POINT('Ctrl Pts',(17.2899131248678,17.0954568570628,12.1096305941645));
#141139=CARTESIAN_POINT('Ctrl Pts',(17.2199454771428,17.1449466854561,12.11388417205));
#141140=CARTESIAN_POINT('Ctrl Pts',(17.1525850704413,17.1978614502303,12.1181377499354));
#141141=CARTESIAN_POINT('Ctrl Pts',(17.0865305766667,17.2497503590347,12.1223088639134));
#141142=CARTESIAN_POINT('Ctrl Pts',(17.0229835115634,17.3049322938693,12.1264799778913));
#141143=CARTESIAN_POINT('Ctrl Pts',(16.9622836350606,17.3631306533724,12.1306510918693));
#141144=CARTESIAN_POINT('Ctrl Pts',(16.9016041269875,17.421309483854,12.1348208061896));
#141145=CARTESIAN_POINT('Ctrl Pts',(16.8437702418585,17.4825024106647,12.13899052051));
#141146=CARTESIAN_POINT('Ctrl Pts',(16.789086714705,17.5463942470714,12.1431602348304));
#141147=CARTESIAN_POINT('Ctrl Pts',(16.734405133426,17.6102838099324,12.1473298007744));
#141148=CARTESIAN_POINT('Ctrl Pts',(16.6828739857151,17.6768717413838,12.1514993667185));
#141149=CARTESIAN_POINT('Ctrl Pts',(16.6347584444193,17.7458089232721,12.1556689326625));
#141150=CARTESIAN_POINT('Ctrl Pts',(16.5849512200484,17.8171698514323,12.1599850954014));
#141151=CARTESIAN_POINT('Ctrl Pts',(16.5388045582795,17.8910478705134,12.1643012581403));
#141152=CARTESIAN_POINT('Ctrl Pts',(16.496563301095,17.9670237066595,12.1686174208793));
#141153=CARTESIAN_POINT('Ctrl Pts',(16.4556980484203,18.0405246379344,12.1727929850709));
#141154=CARTESIAN_POINT('Ctrl Pts',(16.4184878365309,18.1159883689942,12.1769685492626));
#141155=CARTESIAN_POINT('Ctrl Pts',(16.3851063117011,18.1930125535796,12.1811441134543));
#141156=CARTESIAN_POINT('Ctrl Pts',(16.3500387654091,18.2739270466208,12.1855305754669));
#141157=CARTESIAN_POINT('Ctrl Pts',(16.3191970489119,18.3565632259542,12.1899170374794));
#141158=CARTESIAN_POINT('Ctrl Pts',(16.2927234637602,18.4404360029142,12.1943034994919));
#141159=CARTESIAN_POINT('Ctrl Pts',(16.2662498786085,18.5243087798742,12.1986899615045));
#141160=CARTESIAN_POINT('Ctrl Pts',(16.2441444970407,18.6094175737551,12.203076423517));
#141161=CARTESIAN_POINT('Ctrl Pts',(16.2264874578015,18.6952666864385,12.2074628855296));
#141162=CARTESIAN_POINT('Ctrl Pts',(16.2025156137663,18.811818590295,12.2134181072293));
#141163=CARTESIAN_POINT('Ctrl Pts',(16.1866633864877,18.9300931627176,12.219373328929));
#141164=CARTESIAN_POINT('Ctrl Pts',(16.1791211348988,19.0491544419537,12.2253285506288));
#141165=CARTESIAN_POINT('Ctrl Pts',(16.1757600463661,19.10221227165,12.2279824036764));
#141166=CARTESIAN_POINT('Ctrl Pts',(16.1740486686438,19.1554260264049,12.2306362567239));
#141167=CARTESIAN_POINT('Ctrl Pts',(16.174001023388,19.2087109509454,12.2332901097715));
#141168=CARTESIAN_POINT('',(16.1740007840082,19.2130035272629,12.1667098902285));
#141169=CARTESIAN_POINT('Ctrl Pts',(20.2935357313021,17.1808649545431,11.8833305127049));
#141170=CARTESIAN_POINT('Ctrl Pts',(20.2268566426188,17.1296425387906,11.8875000056864));
#141171=CARTESIAN_POINT('Ctrl Pts',(20.1576368380672,17.0816975104457,11.8916694986678));
#141172=CARTESIAN_POINT('Ctrl Pts',(20.0862361972163,17.0372803154643,11.8958389916493));
#141173=CARTESIAN_POINT('Ctrl Pts',(20.0148284810753,16.9928587190582,11.9000088977976));
#141174=CARTESIAN_POINT('Ctrl Pts',(19.9412398908411,16.9519658920357,11.9041788039458));
#141175=CARTESIAN_POINT('Ctrl Pts',(19.8658573577931,16.9148077341804,11.9083487100941));
#141176=CARTESIAN_POINT('Ctrl Pts',(19.7903948874427,16.8776101729941,11.9125230381029));
#141177=CARTESIAN_POINT('Ctrl Pts',(19.7131350895596,16.8441553918421,11.9166973661117));
#141178=CARTESIAN_POINT('Ctrl Pts',(19.6344869976528,16.814602043262,11.9208716941205));
#141179=CARTESIAN_POINT('Ctrl Pts',(19.5557947353724,16.785032096918,11.9250483665171));
#141180=CARTESIAN_POINT('Ctrl Pts',(19.4757130648504,16.7593680861741,11.9292250389137));
#141181=CARTESIAN_POINT('Ctrl Pts',(19.3946660667926,16.7377187082362,11.9334017113104));
#141182=CARTESIAN_POINT('Ctrl Pts',(19.3134800357285,16.7160321916235,11.9375855486277));
#141183=CARTESIAN_POINT('Ctrl Pts',(19.2313258199933,16.6983741580632,11.9417693859451));
#141184=CARTESIAN_POINT('Ctrl Pts',(19.1486372983812,16.6848020840023,11.9459532232625));
#141185=CARTESIAN_POINT('Ctrl Pts',(19.0921615511293,16.6755324416214,11.9488107581933));
#141186=CARTESIAN_POINT('Ctrl Pts',(19.0354367169183,16.6681677363091,11.9516682931241));
#141187=CARTESIAN_POINT('Ctrl Pts',(18.9786013944249,16.662712308658,11.9545258280548));
#141188=CARTESIAN_POINT('Ctrl Pts',(18.8953705500055,16.6547232653983,11.9587104624479));
#141189=CARTESIAN_POINT('Ctrl Pts',(18.8115930039275,16.6508013065455,11.9628950968409));
#141190=CARTESIAN_POINT('Ctrl Pts',(18.7277003248361,16.6510077511655,11.967079731234));
#141191=CARTESIAN_POINT('Ctrl Pts',(18.6439270565892,16.6512139019371,11.9712584093179));
#141192=CARTESIAN_POINT('Ctrl Pts',(18.5600394369382,16.655536782935,11.9754370874019));
#141193=CARTESIAN_POINT('Ctrl Pts',(18.476474237527,16.6639859675175,11.9796157654858));
#141194=CARTESIAN_POINT('Ctrl Pts',(18.3914111919738,16.6725865976613,11.9838693433713));
#141195=CARTESIAN_POINT('Ctrl Pts',(18.306682719051,16.6854629604529,11.9881229212567));
#141196=CARTESIAN_POINT('Ctrl Pts',(18.2227496524044,16.7025695979192,11.9923764991421));
#141197=CARTESIAN_POINT('Ctrl Pts',(18.1404437920366,16.7193445898373,11.9965476131201));
#141198=CARTESIAN_POINT('Ctrl Pts',(18.0589032436843,16.7401871997927,12.0007187270981));
#141199=CARTESIAN_POINT('Ctrl Pts',(17.9785557081123,16.7650024689599,12.004889841076));
#141200=CARTESIAN_POINT('Ctrl Pts',(17.8982351339319,16.7898094111239,12.0090595553964));
#141201=CARTESIAN_POINT('Ctrl Pts',(17.819107216657,16.8185862293725,12.0132292697168));
#141202=CARTESIAN_POINT('Ctrl Pts',(17.7415856439031,16.8511877731877,12.0173989840371));
#141203=CARTESIAN_POINT('Ctrl Pts',(17.6640668296994,16.8837881569001,12.0215685499812));
#141204=CARTESIAN_POINT('Ctrl Pts',(17.5881546700955,16.9202128164544,12.0257381159252));
#141205=CARTESIAN_POINT('Ctrl Pts',(17.5142426975059,16.9602685360061,12.0299076818693));
#141206=CARTESIAN_POINT('Ctrl Pts',(17.4377320711404,17.0017325652431,12.0342238446082));
#141207=CARTESIAN_POINT('Ctrl Pts',(17.3633653656321,17.047087490087,12.0385400073471));
#141208=CARTESIAN_POINT('Ctrl Pts',(17.2915493867659,17.0960682686242,12.042856170086));
#141209=CARTESIAN_POINT('Ctrl Pts',(17.2220728058575,17.1434535034523,12.0470317342777));
#141210=CARTESIAN_POINT('Ctrl Pts',(17.1549836708366,17.1942316733332,12.0512072984694));
#141211=CARTESIAN_POINT('Ctrl Pts',(17.0906175572634,17.2481209545911,12.0553828626611));
#141212=CARTESIAN_POINT('Ctrl Pts',(17.0230004643096,17.3047320553358,12.0597693246736));
#141213=CARTESIAN_POINT('Ctrl Pts',(16.9583891293618,17.3647764140015,12.0641557866861));
#141214=CARTESIAN_POINT('Ctrl Pts',(16.897128197962,17.4278841925221,12.0685422486987));
#141215=CARTESIAN_POINT('Ctrl Pts',(16.8358672665622,17.4909919710426,12.0729287107112));
#141216=CARTESIAN_POINT('Ctrl Pts',(16.7779570635865,17.5571626827013,12.0773151727237));
#141217=CARTESIAN_POINT('Ctrl Pts',(16.7236914224212,17.6259891410741,12.0817016347363));
#141218=CARTESIAN_POINT('Ctrl Pts',(16.6719732357611,17.6915845997261,12.0858821780095));
#141219=CARTESIAN_POINT('Ctrl Pts',(16.62336875941,17.759841108002,12.0900627212828));
#141220=CARTESIAN_POINT('Ctrl Pts',(16.5781640651477,17.8304307616062,12.094243264556));
#141221=CARTESIAN_POINT('Ctrl Pts',(16.5330221281563,17.9009224162283,12.0984180040186));
#141222=CARTESIAN_POINT('Ctrl Pts',(16.4912708487475,17.9737404018919,12.1025927434812));
#141223=CARTESIAN_POINT('Ctrl Pts',(16.4531558825329,18.0485241457064,12.1067674829438));
#141224=CARTESIAN_POINT('Ctrl Pts',(16.4150823671077,18.1232265607011,12.1109376822935));
#141225=CARTESIAN_POINT('Ctrl Pts',(16.3806375190246,18.1998900805266,12.1151078816433));
#141226=CARTESIAN_POINT('Ctrl Pts',(16.350022764859,18.2781267276155,12.1192780809931));
#141227=CARTESIAN_POINT('Ctrl Pts',(16.3194306012405,18.3563056440868,12.1234452031636));
#141228=CARTESIAN_POINT('Ctrl Pts',(16.2926630858421,18.4360549550053,12.1276123253342));
#141229=CARTESIAN_POINT('Ctrl Pts',(16.2698743296475,18.5169649283287,12.1317794475047));
#141230=CARTESIAN_POINT('Ctrl Pts',(16.2470959536793,18.597838047344,12.1359446715606));
#141231=CARTESIAN_POINT('Ctrl Pts',(16.2282928589741,18.6798703351889,12.1401098956165));
#141232=CARTESIAN_POINT('Ctrl Pts',(16.2135694673997,18.7626363860258,12.1442751196725));
#141233=CARTESIAN_POINT('Ctrl Pts',(16.1988435352844,18.8454167182549,12.1484410624433));
#141234=CARTESIAN_POINT('Ctrl Pts',(16.1881988016352,18.9289306143268,12.1526070052142));
#141235=CARTESIAN_POINT('Ctrl Pts',(16.181688476361,19.0127428783137,12.1567729479851));
#141236=CARTESIAN_POINT('Ctrl Pts',(16.1765121589546,19.0793814658902,12.1600852620662));
#141237=CARTESIAN_POINT('Ctrl Pts',(16.1739485082683,19.146208402676,12.1633975761474));
#141238=CARTESIAN_POINT('Ctrl Pts',(16.1740007840082,19.2130035272629,12.1667098902285));
#141239=CARTESIAN_POINT('Ctrl Pts',(16.1763509819005,19.2130199893541,12.1667107986141));
#141240=CARTESIAN_POINT('Ctrl Pts',(16.174290235218,19.4962014494758,12.1807663462153));
#141241=CARTESIAN_POINT('Ctrl Pts',(16.3483939114844,20.6310006362221,12.237213829377));
#141242=CARTESIAN_POINT('Ctrl Pts',(18.0121684955946,22.150770613565,12.3360532480991));
#141243=CARTESIAN_POINT('Ctrl Pts',(20.8151681545049,21.409188138856,12.4632290547806));
#141244=CARTESIAN_POINT('Ctrl Pts',(21.6282770636252,18.8995173227485,12.5789421032606));
#141245=CARTESIAN_POINT('Ctrl Pts',(20.782749801677,17.5654744033761,12.6522632161801));
#141246=CARTESIAN_POINT('Ctrl Pts',(20.2929505239237,17.1816081970507,12.6831923935391));
#141247=CARTESIAN_POINT('Origin',(18.734,19.211,-1.76670989022852));
#141248=CARTESIAN_POINT('',(20.2935357313021,17.1808649545431,13.5498657053664));
#141249=CARTESIAN_POINT('',(20.2935357313021,17.1808649545432,13.4833228577974));
#141250=CARTESIAN_POINT('',(20.2935357313021,17.1808649545432,-1.76670989022852));
#141251=CARTESIAN_POINT('',(16.174000001606,19.2109093211998,13.0332901097364));
#141252=CARTESIAN_POINT('Ctrl Pts',(16.174000001606,19.2109093219104,13.0332901097715));
#141253=CARTESIAN_POINT('Ctrl Pts',(16.1739968821085,19.2989781543512,13.0376462156856));
#141254=CARTESIAN_POINT('Ctrl Pts',(16.1785426714359,19.3869643923453,13.0420023215996));
#141255=CARTESIAN_POINT('Ctrl Pts',(16.1875860737585,19.4743934627951,13.0463584275137));
#141256=CARTESIAN_POINT('Ctrl Pts',(16.1966529338893,19.5620493167382,13.0507258327921));
#141257=CARTESIAN_POINT('Ctrl Pts',(16.2102406836426,19.6491447181138,13.0550932380704));
#141258=CARTESIAN_POINT('Ctrl Pts',(16.2282463851319,19.7352125728895,13.0594606433488));
#141259=CARTESIAN_POINT('Ctrl Pts',(16.2462755658189,19.8213926590147,13.0638337436661));
#141260=CARTESIAN_POINT('Ctrl Pts',(16.2687340840994,19.9065421429603,13.0682068439834));
#141261=CARTESIAN_POINT('Ctrl Pts',(16.2954690366782,19.9902090482795,13.0725799443008));
#141262=CARTESIAN_POINT('Ctrl Pts',(16.3222767415773,20.0741036316347,13.0769649448896));
#141263=CARTESIAN_POINT('Ctrl Pts',(16.3533840099471,20.1565071961889,13.0813499454785));
#141264=CARTESIAN_POINT('Ctrl Pts',(16.3885892814888,20.2369866283206,13.0857349460673));
#141265=CARTESIAN_POINT('Ctrl Pts',(16.4205927188907,20.310146651112,13.0897211414781));
#141266=CARTESIAN_POINT('Ctrl Pts',(16.4559819492917,20.3817167133684,13.0937073368888));
#141267=CARTESIAN_POINT('Ctrl Pts',(16.4945737975983,20.4513911818441,13.0976935322996));
#141268=CARTESIAN_POINT('Ctrl Pts',(16.5350868078939,20.524534153289,13.1018781666926));
#141269=CARTESIAN_POINT('Ctrl Pts',(16.5792624158945,20.5958263313022,13.1060628010857));
#141270=CARTESIAN_POINT('Ctrl Pts',(16.6269069559,20.6648771968449,13.1102474354787));
#141271=CARTESIAN_POINT('Ctrl Pts',(16.6744836798,20.7338297770272,13.1144261135626));
#141272=CARTESIAN_POINT('Ctrl Pts',(16.7255192690591,20.8005470061347,13.1186047916466));
#141273=CARTESIAN_POINT('Ctrl Pts',(16.7797744504213,20.8646633579341,13.1227834697305));
#141274=CARTESIAN_POINT('Ctrl Pts',(16.8350021169169,20.9299289492599,13.127037047616));
#141275=CARTESIAN_POINT('Ctrl Pts',(16.8935656995718,20.9924990829437,13.1312906255014));
#141276=CARTESIAN_POINT('Ctrl Pts',(16.9551669364597,21.0520195360332,13.1355442033868));
#141277=CARTESIAN_POINT('Ctrl Pts',(17.0155739131657,21.110386068995,13.1397153173648));
#141278=CARTESIAN_POINT('Ctrl Pts',(17.0789014673909,21.1658197797781,13.1438864313427));
#141279=CARTESIAN_POINT('Ctrl Pts',(17.1448292745178,21.2180217749866,13.1480575453207));
#141280=CARTESIAN_POINT('Ctrl Pts',(17.2107349589323,21.2702062533115,13.1522272596411));
#141281=CARTESIAN_POINT('Ctrl Pts',(17.279238803008,21.3191608844269,13.1563969739614));
#141282=CARTESIAN_POINT('Ctrl Pts',(17.3499870301186,21.364626731632,13.1605666882818));
#141283=CARTESIAN_POINT('Ctrl Pts',(17.4207327397037,21.4100909609672,13.1647362542259));
#141284=CARTESIAN_POINT('Ctrl Pts',(17.493722286064,21.4520664052353,13.1689058201699));
#141285=CARTESIAN_POINT('Ctrl Pts',(17.5685736694553,21.490337945122,13.1730753861139));
#141286=CARTESIAN_POINT('Ctrl Pts',(17.6460567351475,21.5299550651381,13.1773915488529));
#141287=CARTESIAN_POINT('Ctrl Pts',(17.7255345286225,21.5656027360313,13.1817077115918));
#141288=CARTESIAN_POINT('Ctrl Pts',(17.8065583197873,21.5970955407955,13.1860238743307));
#141289=CARTESIAN_POINT('Ctrl Pts',(17.8849427694771,21.627562470757,13.1901994385224));
#141290=CARTESIAN_POINT('Ctrl Pts',(17.9647735800336,21.654140963194,13.1943750027141));
#141291=CARTESIAN_POINT('Ctrl Pts',(18.0456284938942,21.6767138255648,13.1985505669057));
#141292=CARTESIAN_POINT('Ctrl Pts',(18.1305671972396,21.7004267895521,13.2029370289183));
#141293=CARTESIAN_POINT('Ctrl Pts',(18.2166356079045,21.7197187126534,13.2073234909308));
#141294=CARTESIAN_POINT('Ctrl Pts',(18.3033337697291,21.7345147311051,13.2117099529434));
#141295=CARTESIAN_POINT('Ctrl Pts',(18.3900319315536,21.7493107495567,13.2160964149559));
#141296=CARTESIAN_POINT('Ctrl Pts',(18.4773592594052,21.7596108709354,13.2204828769685));
#141297=CARTESIAN_POINT('Ctrl Pts',(18.5648137584886,21.7654032601927,13.224869338981));
#141298=CARTESIAN_POINT('Ctrl Pts',(18.6482443464305,21.7709291330339,13.2290539733741));
#141299=CARTESIAN_POINT('Ctrl Pts',(18.7321012046618,21.7723735414423,13.2332386077671));
#141300=CARTESIAN_POINT('Ctrl Pts',(18.8159511409016,21.7696879470746,13.2374232421601));
#141301=CARTESIAN_POINT('Ctrl Pts',(18.8996817271358,21.7670061753181,13.2416019202441));
#141302=CARTESIAN_POINT('Ctrl Pts',(18.9834049550843,21.7602060920318,13.2457805983281));
#141303=CARTESIAN_POINT('Ctrl Pts',(19.0666839609554,21.749291035741,13.249959276412));
#141304=CARTESIAN_POINT('Ctrl Pts',(19.1514556831552,21.7381803349106,13.2542128542974));
#141305=CARTESIAN_POINT('Ctrl Pts',(19.2357666201898,21.7228056564124,13.2584664321829));
#141306=CARTESIAN_POINT('Ctrl Pts',(19.3191574830897,21.7032260571594,13.2627200100683));
#141307=CARTESIAN_POINT('Ctrl Pts',(19.4009316513884,21.6840260466443,13.2668911240463));
#141308=CARTESIAN_POINT('Ctrl Pts',(19.4818206335821,21.660782811607,13.2710622380242));
#141309=CARTESIAN_POINT('Ctrl Pts',(19.5613997219857,21.6336039090322,13.2752333520022));
#141310=CARTESIAN_POINT('Ctrl Pts',(19.6409521068576,21.6064341266006,13.2794030663225));
#141311=CARTESIAN_POINT('Ctrl Pts',(19.7191950359073,21.5753314480261,13.2835727806429));
#141312=CARTESIAN_POINT('Ctrl Pts',(19.7957192917692,21.5404531859398,13.2877424949633));
#141313=CARTESIAN_POINT('Ctrl Pts',(19.8722408245697,21.5055761649718,13.2919120609073));
#141314=CARTESIAN_POINT('Ctrl Pts',(19.9470433875298,21.466924019184,13.2960816268514));
#141315=CARTESIAN_POINT('Ctrl Pts',(20.019739330133,21.4247015099035,13.3002511927954));
#141316=CARTESIAN_POINT('Ctrl Pts',(20.0949911723979,21.380994509284,13.3045673555344));
#141317=CARTESIAN_POINT('Ctrl Pts',(20.1679850444452,21.333461670748,13.3088835182733));
#141318=CARTESIAN_POINT('Ctrl Pts',(20.2383221508272,21.2823799425819,13.3131996810122));
#141319=CARTESIAN_POINT('Ctrl Pts',(20.3063680333671,21.232962196338,13.3173752452039));
#141320=CARTESIAN_POINT('Ctrl Pts',(20.3719272430122,21.1802235520147,13.3215508093956));
#141321=CARTESIAN_POINT('Ctrl Pts',(20.4346726793712,21.1244556272986,13.3257263735873));
#141322=CARTESIAN_POINT('Ctrl Pts',(20.5005872385574,21.0658709972807,13.3301128355998));
#141323=CARTESIAN_POINT('Ctrl Pts',(20.5633958911488,21.0039434366074,13.3344992976123));
#141324=CARTESIAN_POINT('Ctrl Pts',(20.6227650717808,20.9390528069538,13.3388857596249));
#141325=CARTESIAN_POINT('Ctrl Pts',(20.6821342524128,20.8741621773001,13.3432722216374));
#141326=CARTESIAN_POINT('Ctrl Pts',(20.738063650735,20.8063089747713,13.3476586836499));
#141327=CARTESIAN_POINT('Ctrl Pts',(20.7902715950829,20.7359088914605,13.3520451456625));
#141328=CARTESIAN_POINT('Ctrl Pts',(20.8400773745207,20.6687480203406,13.3562297800555));
#141329=CARTESIAN_POINT('Ctrl Pts',(20.8866820202991,20.5990195040797,13.3604144144486));
#141330=CARTESIAN_POINT('Ctrl Pts',(20.9298102405871,20.5270613159472,13.3645990488416));
#141331=CARTESIAN_POINT('Ctrl Pts',(20.9728770731919,20.4552055513888,13.3687777269256));
#141332=CARTESIAN_POINT('Ctrl Pts',(21.0124770746366,20.3811268100631,13.3729564050095));
#141333=CARTESIAN_POINT('Ctrl Pts',(21.0483765860078,20.305194232364,13.3771350830935));
#141334=CARTESIAN_POINT('Ctrl Pts',(21.0849195703199,20.2279006177816,13.3813886609789));
#141335=CARTESIAN_POINT('Ctrl Pts',(21.1176278099319,20.1486864403633,13.3856422388643));
#141336=CARTESIAN_POINT('Ctrl Pts',(21.1463023579538,20.0679698558354,13.3898958167498));
#141337=CARTESIAN_POINT('Ctrl Pts',(21.1744209939084,19.9888181198042,13.3940669307277));
#141338=CARTESIAN_POINT('Ctrl Pts',(21.1986607834443,19.9082221644555,13.3982380447057));
#141339=CARTESIAN_POINT('Ctrl Pts',(21.2188822787495,19.8265973202968,13.4024091586836));
#141340=CARTESIAN_POINT('Ctrl Pts',(21.2390969885367,19.7449998661428,13.406578873004));
#141341=CARTESIAN_POINT('Ctrl Pts',(21.2552959714612,19.6623746550205,13.4107485873244));
#141342=CARTESIAN_POINT('Ctrl Pts',(21.2673900009521,19.5791509243179,13.4149183016447));
#141343=CARTESIAN_POINT('Ctrl Pts',(21.2794836000854,19.4959301550728,13.4190878675888));
#141344=CARTESIAN_POINT('Ctrl Pts',(21.2874724709,19.4121113639667,13.4232574335328));
#141345=CARTESIAN_POINT('Ctrl Pts',(21.2913189573957,19.3281313371595,13.4274269994769));
#141346=CARTESIAN_POINT('Ctrl Pts',(21.2953006816113,19.2411986762104,13.4317431622158));
#141347=CARTESIAN_POINT('Ctrl Pts',(21.2948432851383,19.1540937573814,13.4360593249547));
#141348=CARTESIAN_POINT('Ctrl Pts',(21.2899637772452,19.0673018113878,13.4403754876936));
#141349=CARTESIAN_POINT('Ctrl Pts',(21.2852432188086,18.9833371039062,13.4445510518853));
#141350=CARTESIAN_POINT('Ctrl Pts',(21.2763843217563,18.89966575566,13.448726616077));
#141351=CARTESIAN_POINT('Ctrl Pts',(21.2634552371753,18.8167206534363,13.4529021802687));
#141352=CARTESIAN_POINT('Ctrl Pts',(21.249873135268,18.7295861912825,13.4572886422812));
#141353=CARTESIAN_POINT('Ctrl Pts',(21.2317989893781,18.6432538400943,13.4616751042937));
#141354=CARTESIAN_POINT('Ctrl Pts',(21.2093716504547,18.5582096874759,13.4660615663063));
#141355=CARTESIAN_POINT('Ctrl Pts',(21.1869443115313,18.4731655348574,13.4704480283188));
#141356=CARTESIAN_POINT('Ctrl Pts',(21.1601640287335,18.3894101102965,13.4748344903314));
#141357=CARTESIAN_POINT('Ctrl Pts',(21.1292278697973,18.3074052613331,13.4792209523439));
#141358=CARTESIAN_POINT('Ctrl Pts',(21.099717216383,18.2291791091776,13.4834052908209));
#141359=CARTESIAN_POINT('Ctrl Pts',(21.066315417783,18.1522546019502,13.4875896292979));
#141360=CARTESIAN_POINT('Ctrl Pts',(21.0291576153336,18.0770460676129,13.4917739677749));
#141361=CARTESIAN_POINT('Ctrl Pts',(20.992050293613,18.0019397078225,13.4959526216193));
#141362=CARTESIAN_POINT('Ctrl Pts',(20.951197302462,17.9285451006079,13.5001312754636));
#141363=CARTESIAN_POINT('Ctrl Pts',(20.906782548638,17.8572585193863,13.504309929308));
#141364=CARTESIAN_POINT('Ctrl Pts',(20.8624197060777,17.7860552567964,13.5084836992077));
#141365=CARTESIAN_POINT('Ctrl Pts',(20.8145036177023,17.7169555110608,13.5126574691073));
#141366=CARTESIAN_POINT('Ctrl Pts',(20.7632642938687,17.6503314171069,13.516831239007));
#141367=CARTESIAN_POINT('Ctrl Pts',(20.7120601643926,17.5837530847285,13.5210021421017));
#141368=CARTESIAN_POINT('Ctrl Pts',(20.6575376129952,17.5196473901183,13.5251730451963));
#141369=CARTESIAN_POINT('Ctrl Pts',(20.5999695483242,17.4583569545607,13.529343948291));
#141370=CARTESIAN_POINT('Ctrl Pts',(20.5424157972193,17.3970817580893,13.5335138143437));
#141371=CARTESIAN_POINT('Ctrl Pts',(20.481818346985,17.338620769584,13.5376836803964));
#141372=CARTESIAN_POINT('Ctrl Pts',(20.4184891456858,17.2832820958276,13.5418535464492));
#141373=CARTESIAN_POINT('Ctrl Pts',(20.3779280006757,17.2478387312367,13.5445242660882));
#141374=CARTESIAN_POINT('Ctrl Pts',(20.3362470303383,17.2136754796983,13.5471949857273));
#141375=CARTESIAN_POINT('Ctrl Pts',(20.2935357313021,17.1808649545431,13.5498657053664));
#141376=CARTESIAN_POINT('Ctrl Pts',(20.2935357313021,17.1808649545432,12.7499597618547));
#141377=CARTESIAN_POINT('Ctrl Pts',(20.2269466206031,17.1297116592572,12.7541315981782));
#141378=CARTESIAN_POINT('Ctrl Pts',(20.1577807292293,17.0817939555633,12.7583034345017));
#141379=CARTESIAN_POINT('Ctrl Pts',(20.0863882141111,17.0373748901125,12.7624752708252));
#141380=CARTESIAN_POINT('Ctrl Pts',(20.0150265963101,16.992975048385,12.7666453016577));
#141381=CARTESIAN_POINT('Ctrl Pts',(19.9414406583524,16.9520710809438,12.7708153324901));
#141382=CARTESIAN_POINT('Ctrl Pts',(19.8660096487203,16.9148828089133,12.7749853633225));
#141383=CARTESIAN_POINT('Ctrl Pts',(19.7905886566178,16.8776994756289,12.7791548403587));
#141384=CARTESIAN_POINT('Ctrl Pts',(19.7133234924244,16.8442310603422,12.7833243173949));
#141385=CARTESIAN_POINT('Ctrl Pts',(19.6346168965686,16.8146508589909,12.7874937944311));
#141386=CARTESIAN_POINT('Ctrl Pts',(19.555897143493,16.7850657127781,12.7916639684702));
#141387=CARTESIAN_POINT('Ctrl Pts',(19.4757359113357,16.7593702317383,12.7958341425094));
#141388=CARTESIAN_POINT('Ctrl Pts',(19.3945534566075,16.7376886304058,12.8000043165485));
#141389=CARTESIAN_POINT('Ctrl Pts',(19.3132817042356,16.7159831801282,12.804179077622));
#141390=CARTESIAN_POINT('Ctrl Pts',(19.2309869325325,16.6983005401868,12.8083538386956));
#141391=CARTESIAN_POINT('Ctrl Pts',(19.1481014831742,16.6847141963679,12.8125285997691));
#141392=CARTESIAN_POINT('Ctrl Pts',(19.0651644239002,16.6711193928005,12.8167059603227));
#141393=CARTESIAN_POINT('Ctrl Pts',(18.9816364116983,16.6616260140211,12.8208833208762));
#141394=CARTESIAN_POINT('Ctrl Pts',(18.8979544455511,16.6562556018685,12.8250606814298));
#141395=CARTESIAN_POINT('Ctrl Pts',(18.8141346488939,16.6508763442422,12.8292449224112));
#141396=CARTESIAN_POINT('Ctrl Pts',(18.7301608515015,16.6496336145246,12.8334291633927));
#141397=CARTESIAN_POINT('Ctrl Pts',(18.6464691460235,16.6524968537049,12.8376134043741));
#141398=CARTESIAN_POINT('Ctrl Pts',(18.6082759065393,16.6538035110264,12.8395229092283));
#141399=CARTESIAN_POINT('Ctrl Pts',(18.5701413311388,16.6559645682452,12.8414324140825));
#141400=CARTESIAN_POINT('Ctrl Pts',(18.5321062576876,16.6589735665916,12.8433419189367));
#141401=CARTESIAN_POINT('Ctrl Pts',(18.4487533004234,16.665567714777,12.8475265533297));
#141402=CARTESIAN_POINT('Ctrl Pts',(18.3655686284662,16.6762620749485,12.8517111877228));
#141403=CARTESIAN_POINT('Ctrl Pts',(18.2829879003452,16.6910420467863,12.8558958221158));
#141404=CARTESIAN_POINT('Ctrl Pts',(18.2005247156691,16.7058009811636,12.8600745001998));
#141405=CARTESIAN_POINT('Ctrl Pts',(18.1186642162791,16.7246338957134,12.8642531782837));
#141406=CARTESIAN_POINT('Ctrl Pts',(18.0378381935504,16.7474743274646,12.8684318563677));
#141407=CARTESIAN_POINT('Ctrl Pts',(17.9555634224531,16.7707241575398,12.8726854342531));
#141408=CARTESIAN_POINT('Ctrl Pts',(17.8743610594189,16.7981265494107,12.8769390121385));
#141409=CARTESIAN_POINT('Ctrl Pts',(17.794677029921,16.8295566649861,12.881192590024));
#141410=CARTESIAN_POINT('Ctrl Pts',(17.7165378308257,16.8603774464402,12.8853637040019));
#141411=CARTESIAN_POINT('Ctrl Pts',(17.6398590665653,16.8950709981006,12.8895348179799));
#141412=CARTESIAN_POINT('Ctrl Pts',(17.5650454327531,16.933469490937,12.8937059319578));
#141413=CARTESIAN_POINT('Ctrl Pts',(17.4902569033782,16.9718550987884,12.8978756462782));
#141414=CARTESIAN_POINT('Ctrl Pts',(17.4173326704111,17.0139429688571,12.9020453605985));
#141415=CARTESIAN_POINT('Ctrl Pts',(17.3466549084732,17.0595182787166,12.9062150749189));
#141416=CARTESIAN_POINT('Ctrl Pts',(17.2759796615534,17.1050919668111,12.9103846408629));
#141417=CARTESIAN_POINT('Ctrl Pts',(17.2075511128835,17.1541525979349,12.914554206807));
#141418=CARTESIAN_POINT('Ctrl Pts',(17.1417232369316,17.2064415174926,12.918723772751));
#141419=CARTESIAN_POINT('Ctrl Pts',(17.0735809340684,17.2605688509567,12.9230399354899));
#141420=CARTESIAN_POINT('Ctrl Pts',(17.0082259988606,17.3181553818451,12.9273560982289));
#141421=CARTESIAN_POINT('Ctrl Pts',(16.946012997198,17.3788694157317,12.9316722609678));
#141422=CARTESIAN_POINT('Ctrl Pts',(16.8858265775211,17.4376056963503,12.9358478251595));
#141423=CARTESIAN_POINT('Ctrl Pts',(16.8285808237901,17.4992684748645,12.9400233893511));
#141424=CARTESIAN_POINT('Ctrl Pts',(16.77455723925,17.5635219068696,12.9441989535428));
#141425=CARTESIAN_POINT('Ctrl Pts',(16.7178050518835,17.6310206269775,12.9485854155554));
#141426=CARTESIAN_POINT('Ctrl Pts',(16.6646094437671,17.7013781204553,12.9529718775679));
#141427=CARTESIAN_POINT('Ctrl Pts',(16.6152455573351,17.7741702913401,12.9573583395805));
#141428=CARTESIAN_POINT('Ctrl Pts',(16.565881670903,17.846962462225,12.961744801593));
#141429=CARTESIAN_POINT('Ctrl Pts',(16.5203497415207,17.922188774755,12.9661312636056));
#141430=CARTESIAN_POINT('Ctrl Pts',(16.4788683829465,17.9993971815129,12.9705177256181));
#141431=CARTESIAN_POINT('Ctrl Pts',(16.4371381237559,18.0770688619124,12.9749305077209));
#141432=CARTESIAN_POINT('Ctrl Pts',(16.3993648293881,18.1570094498413,12.9793432898236));
#141433=CARTESIAN_POINT('Ctrl Pts',(16.3657873879884,18.2388019624021,12.9837560719264));
#141434=CARTESIAN_POINT('Ctrl Pts',(16.3323070847556,18.3203578525641,12.9881560880307));
#141435=CARTESIAN_POINT('Ctrl Pts',(16.3029985969533,18.4037546379833,12.992556104135));
#141436=CARTESIAN_POINT('Ctrl Pts',(16.2780542372553,18.4885524860197,12.9969561202393));
#141437=CARTESIAN_POINT('Ctrl Pts',(16.2531532512187,18.5732028861683,13.0013484855236));
#141438=CARTESIAN_POINT('Ctrl Pts',(16.2326014031163,18.6592491335653,13.0057408508078));
#141439=CARTESIAN_POINT('Ctrl Pts',(16.2165427462274,18.7462323425329,13.010133216092));
#141440=CARTESIAN_POINT('Ctrl Pts',(16.2005210016679,18.833015612434,13.0145154851125));
#141441=CARTESIAN_POINT('Ctrl Pts',(16.1889719431304,18.9207311752712,13.018897754133));
#141442=CARTESIAN_POINT('Ctrl Pts',(16.1819893075699,19.0089073833058,13.0232800231536));
#141443=CARTESIAN_POINT('Ctrl Pts',(16.176672671659,19.0760454703589,13.0266167186812));
#141444=CARTESIAN_POINT('Ctrl Pts',(16.1740023911013,19.1434502453368,13.0299534142088));
#141445=CARTESIAN_POINT('Ctrl Pts',(16.174000001606,19.2109093211998,13.0332901097364));
#141446=CARTESIAN_POINT('',(16.1736697067219,19.2116425106688,12.9667098340815));
#141447=CARTESIAN_POINT('Ctrl Pts',(20.2929505239237,17.1816081970507,12.6831923935391));
#141448=CARTESIAN_POINT('Ctrl Pts',(20.1114244968023,17.0393423535811,12.6946551517406));
#141449=CARTESIAN_POINT('Ctrl Pts',(19.1726622027867,16.486376634711,12.7485098455025));
#141450=CARTESIAN_POINT('Ctrl Pts',(17.0319370398065,16.7305239353302,12.8430154491721));
#141451=CARTESIAN_POINT('Ctrl Pts',(16.1727139355615,18.3978728515243,12.9260582946402));
#141452=CARTESIAN_POINT('Ctrl Pts',(16.1699654719056,19.2116308397489,12.9667092045479));
#141453=CARTESIAN_POINT('Ctrl Pts',(16.1740000808904,19.2116435515775,12.9667098902285));
#141454=CARTESIAN_POINT('Ctrl Pts',(16.1740088273484,19.2464363059256,12.9684506873211));
#141455=CARTESIAN_POINT('Ctrl Pts',(16.1747268399112,19.281219269613,12.9701914844137));
#141456=CARTESIAN_POINT('Ctrl Pts',(16.1761531171477,19.3159729673894,12.9719322815063));
#141457=CARTESIAN_POINT('Ctrl Pts',(16.1795816894971,19.3995160291397,12.9761169158993));
#141458=CARTESIAN_POINT('Ctrl Pts',(16.1871139062631,19.4830464110296,12.9803015502924));
#141459=CARTESIAN_POINT('Ctrl Pts',(16.1987516982625,19.5661282142232,12.9844861846854));
#141460=CARTESIAN_POINT('Ctrl Pts',(16.2103729253056,19.6490917607534,12.9886648627694));
#141461=CARTESIAN_POINT('Ctrl Pts',(16.2260880567289,19.7316075451534,12.9928435408533));
#141462=CARTESIAN_POINT('Ctrl Pts',(16.2458470513545,19.8132415662726,12.9970222189372));
#141463=CARTESIAN_POINT('Ctrl Pts',(16.2659602117582,19.896338818551,13.0012757968227));
#141464=CARTESIAN_POINT('Ctrl Pts',(16.2902636140325,19.9785219036749,13.0055293747081));
#141465=CARTESIAN_POINT('Ctrl Pts',(16.3186494198466,20.0593404829151,13.0097829525936));
#141466=CARTESIAN_POINT('Ctrl Pts',(16.3464849114246,20.1385922362921,13.0139540665715));
#141467=CARTESIAN_POINT('Ctrl Pts',(16.3782457689157,20.2165314648406,13.0181251805495));
#141468=CARTESIAN_POINT('Ctrl Pts',(16.4137796304916,20.2927473997743,13.0222962945274));
#141469=CARTESIAN_POINT('Ctrl Pts',(16.4493015683371,20.3689377597149,13.0264660088478));
#141470=CARTESIAN_POINT('Ctrl Pts',(16.4885938016079,20.4434055578922,13.0306357231682));
#141471=CARTESIAN_POINT('Ctrl Pts',(16.5314561548597,20.5157607482732,13.0348054374885));
#141472=CARTESIAN_POINT('Ctrl Pts',(16.574316982885,20.5881133639461,13.0389750034326));
#141473=CARTESIAN_POINT('Ctrl Pts',(16.6207474431038,20.6583531259277,13.0431445693766));
#141474=CARTESIAN_POINT('Ctrl Pts',(16.6705024900496,20.7261165058927,13.0473141353206));
#141475=CARTESIAN_POINT('Ctrl Pts',(16.7220068630667,20.7962623627024,13.0516302980596));
#141476=CARTESIAN_POINT('Ctrl Pts',(16.7770736453881,20.8637540331555,13.0559464607985));
#141477=CARTESIAN_POINT('Ctrl Pts',(16.8353848266791,20.9282246281822,13.0602626235374));
#141478=CARTESIAN_POINT('Ctrl Pts',(16.8917965273727,20.9905951003569,13.0644381877291));
#141479=CARTESIAN_POINT('Ctrl Pts',(16.951244134227,21.0501379976127,13.0686137519208));
#141480=CARTESIAN_POINT('Ctrl Pts',(17.0134027193005,21.1065592836019,13.0727893161124));
#141481=CARTESIAN_POINT('Ctrl Pts',(17.0787007867382,21.1658302746177,13.077175778125));
#141482=CARTESIAN_POINT('Ctrl Pts',(17.1469904406111,21.2216556522274,13.0815622401375));
#141483=CARTESIAN_POINT('Ctrl Pts',(17.2178583236868,21.273744389726,13.0859487021501));
#141484=CARTESIAN_POINT('Ctrl Pts',(17.2887262067624,21.3258331272246,13.0903351641627));
#141485=CARTESIAN_POINT('Ctrl Pts',(17.3621717925896,21.3741849690991,13.0947216261752));
#141486=CARTESIAN_POINT('Ctrl Pts',(17.4377516489582,21.4185643167123,13.0991080881878));
#141487=CARTESIAN_POINT('Ctrl Pts',(17.5098539640988,21.4609017047557,13.1032927225808));
#141488=CARTESIAN_POINT('Ctrl Pts',(17.5841668423744,21.4997817138926,13.1074773569739));
#141489=CARTESIAN_POINT('Ctrl Pts',(17.660324806961,21.5349667768392,13.1116619913669));
#141490=CARTESIAN_POINT('Ctrl Pts',(17.7363743701113,21.5701017582038,13.1158406694508));
#141491=CARTESIAN_POINT('Ctrl Pts',(17.8142633889641,21.6015520487103,13.1200193475348));
#141492=CARTESIAN_POINT('Ctrl Pts',(17.8935998508933,21.629124808479,13.1241980256187));
#141493=CARTESIAN_POINT('Ctrl Pts',(17.9743583618844,21.6571917901503,13.1284516035042));
#141494=CARTESIAN_POINT('Ctrl Pts',(18.0566163014189,21.6812406201864,13.1327051813896));
#141495=CARTESIAN_POINT('Ctrl Pts',(18.1399366350501,21.701118213745,13.136958759275));
#141496=CARTESIAN_POINT('Ctrl Pts',(18.2216416414276,21.7206104413645,13.141129873253));
#141497=CARTESIAN_POINT('Ctrl Pts',(18.3043677482543,21.7360916126581,13.1453009872309));
#141498=CARTESIAN_POINT('Ctrl Pts',(18.3876870934184,21.7474674984582,13.1494721012089));
#141499=CARTESIAN_POINT('Ctrl Pts',(18.4709784799716,21.75883956697,13.1536418155293));
#141500=CARTESIAN_POINT('Ctrl Pts',(18.5548622540875,21.76610902368,13.1578115298496));
#141501=CARTESIAN_POINT('Ctrl Pts',(18.6389020976073,21.7692330599381,13.16198124417));
#141502=CARTESIAN_POINT('Ctrl Pts',(18.7229389506288,21.7723569850297,13.1661508101141));
#141503=CARTESIAN_POINT('Ctrl Pts',(18.8071314022652,21.7713357667235,13.1703203760581));
#141504=CARTESIAN_POINT('Ctrl Pts',(18.8910411442612,21.7661786784898,13.1744899420021));
#141505=CARTESIAN_POINT('Ctrl Pts',(18.9779010492718,21.7608402733959,13.1788061047411));
#141506=CARTESIAN_POINT('Ctrl Pts',(19.0644574681807,21.7510697851064,13.18312226748));
#141507=CARTESIAN_POINT('Ctrl Pts',(19.1502297723789,21.7369360198915,13.1874384302189));
#141508=CARTESIAN_POINT('Ctrl Pts',(19.2332080527895,21.7232626605919,13.1916139944106));
#141509=CARTESIAN_POINT('Ctrl Pts',(19.3154520685912,21.7055060719794,13.1957895586023));
#141510=CARTESIAN_POINT('Ctrl Pts',(19.3965387044155,21.6837803107335,13.1999651227939));
#141511=CARTESIAN_POINT('Ctrl Pts',(19.48172083345,21.6609572329353,13.2043515848065));
#141512=CARTESIAN_POINT('Ctrl Pts',(19.5656250358875,21.6337536591884,13.208738046819));
#141513=CARTESIAN_POINT('Ctrl Pts',(19.6477828618952,21.6023596302745,13.2131245088315));
#141514=CARTESIAN_POINT('Ctrl Pts',(19.7299406879028,21.5709656013606,13.2175109708441));
#141515=CARTESIAN_POINT('Ctrl Pts',(19.8103516376766,21.5353814216376,13.2218974328566));
#141516=CARTESIAN_POINT('Ctrl Pts',(19.8885775886019,21.4958524223455,13.2262838948691));
#141517=CARTESIAN_POINT('Ctrl Pts',(19.9632042475665,21.4581422109069,13.2304685292622));
#141518=CARTESIAN_POINT('Ctrl Pts',(20.0361203339113,21.4167018520732,13.2346531636552));
#141519=CARTESIAN_POINT('Ctrl Pts',(20.1069282654731,21.3717100633507,13.2388377980483));
#141520=CARTESIAN_POINT('Ctrl Pts',(20.1776354107087,21.3267823148705,13.2430164761322));
#141521=CARTESIAN_POINT('Ctrl Pts',(20.2462399765313,21.278313421969,13.2471951542162));
#141522=CARTESIAN_POINT('Ctrl Pts',(20.3123676261203,21.2265286246579,13.2513738323001));
#141523=CARTESIAN_POINT('Ctrl Pts',(20.379680566303,21.1738156220721,13.2556274101856));
#141524=CARTESIAN_POINT('Ctrl Pts',(20.4444264890784,21.1176668881011,13.259880988071));
#141525=CARTESIAN_POINT('Ctrl Pts',(20.5062401158633,21.0583670376308,13.2641345659564));
#141526=CARTESIAN_POINT('Ctrl Pts',(20.5668553648736,21.000216830476,13.2683056799344));
#141527=CARTESIAN_POINT('Ctrl Pts',(20.6246506525837,20.9390369307226,13.2724767939123));
#141528=CARTESIAN_POINT('Ctrl Pts',(20.6793151535296,20.8751360982348,13.2766479078903));
#141529=CARTESIAN_POINT('Ctrl Pts',(20.7339613112743,20.8112567082884,13.2808176222106));
#141530=CARTESIAN_POINT('Ctrl Pts',(20.7854784698982,20.744658548193,13.284987336531));
#141531=CARTESIAN_POINT('Ctrl Pts',(20.8335944633575,20.6756853209609,13.2891570508514));
#141532=CARTESIAN_POINT('Ctrl Pts',(20.8817087446433,20.6067145480924,13.2933266167954));
#141533=CARTESIAN_POINT('Ctrl Pts',(20.9264218388937,20.5353692539103,13.2974961827395));
#141534=CARTESIAN_POINT('Ctrl Pts',(20.9675042956844,20.4620230058473,13.3016657486835));
#141535=CARTESIAN_POINT('Ctrl Pts',(21.0100311609753,20.3860979941847,13.3059819114224));
#141536=CARTESIAN_POINT('Ctrl Pts',(21.0486670744203,20.3080291637333,13.3102980741614));
#141537=CARTESIAN_POINT('Ctrl Pts',(21.0832097360536,20.2282578906212,13.3146142369003));
#141538=CARTESIAN_POINT('Ctrl Pts',(21.1166271741174,20.1510851583403,13.318789801092));
#141539=CARTESIAN_POINT('Ctrl Pts',(21.1462138190076,20.0723196518132,13.3229653652836));
#141540=CARTESIAN_POINT('Ctrl Pts',(21.1718365500182,19.9923788808226,13.3271409294753));
#141541=CARTESIAN_POINT('Ctrl Pts',(21.1987534242598,19.9084004915303,13.3315273914879));
#141542=CARTESIAN_POINT('Ctrl Pts',(21.221295277208,19.8231255568953,13.3359138535004));
#141543=CARTESIAN_POINT('Ctrl Pts',(21.2393683400758,19.7370508345643,13.340300315513));
#141544=CARTESIAN_POINT('Ctrl Pts',(21.2574414029436,19.6509761122332,13.3446867775255));
#141545=CARTESIAN_POINT('Ctrl Pts',(21.2710456611134,19.5641021872051,13.349073239538));
#141546=CARTESIAN_POINT('Ctrl Pts',(21.2801502518719,19.4769302444118,13.3534597015506));
#141547=CARTESIAN_POINT('Ctrl Pts',(21.2888359269133,19.3937692119263,13.3576443359436));
#141548=CARTESIAN_POINT('Ctrl Pts',(21.2934592377886,19.3100274422731,13.3618289703367));
#141549=CARTESIAN_POINT('Ctrl Pts',(21.2939552539536,19.2261359755289,13.3660136047297));
#141550=CARTESIAN_POINT('Ctrl Pts',(21.294450564101,19.1423639179039,13.3701922828137));
#141551=CARTESIAN_POINT('Ctrl Pts',(21.2908302458307,19.0584430425126,13.3743709608976));
#141552=CARTESIAN_POINT('Ctrl Pts',(21.2830810689264,18.9748100255276,13.3785496389816));
#141553=CARTESIAN_POINT('Ctrl Pts',(21.2751929935952,18.8896779468192,13.382803216867));
#141554=CARTESIAN_POINT('Ctrl Pts',(21.2630265340501,18.804844627276,13.3870567947524));
#141555=CARTESIAN_POINT('Ctrl Pts',(21.2466232879999,18.7207712650195,13.3913103726379));
#141556=CARTESIAN_POINT('Ctrl Pts',(21.2305380508827,18.6383278289459,13.3954814866158));
#141557=CARTESIAN_POINT('Ctrl Pts',(21.2103789301822,18.5566156189164,13.3996526005938));
#141558=CARTESIAN_POINT('Ctrl Pts',(21.1862373001536,18.4760631158151,13.4038237145717));
#141559=CARTESIAN_POINT('Ctrl Pts',(21.1621037710821,18.3955376428842,13.4079934288921));
#141560=CARTESIAN_POINT('Ctrl Pts',(21.1339905186921,18.3161715443229,13.4121631432125));
#141561=CARTESIAN_POINT('Ctrl Pts',(21.1020392245073,18.2383797086247,13.4163328575329));
#141562=CARTESIAN_POINT('Ctrl Pts',(21.0700890672866,18.1605906410939,13.4205024234769));
#141563=CARTESIAN_POINT('Ctrl Pts',(21.0343013153839,18.0843761502596,13.4246719894209));
#141564=CARTESIAN_POINT('Ctrl Pts',(20.9948658827287,18.0101313725834,13.428841555365));
#141565=CARTESIAN_POINT('Ctrl Pts',(20.9540439489102,17.933276240115,13.4331577181039));
#141566=CARTESIAN_POINT('Ctrl Pts',(20.9093133043206,17.8585323739429,13.4374738808428));
#141567=CARTESIAN_POINT('Ctrl Pts',(20.8609355752997,17.7863087848504,13.4417900435817));
#141568=CARTESIAN_POINT('Ctrl Pts',(20.8141337457132,17.7164378715759,13.4459656077734));
#141569=CARTESIAN_POINT('Ctrl Pts',(20.7639191093595,17.6489259106341,13.4501411719651));
#141570=CARTESIAN_POINT('Ctrl Pts',(20.7105706701801,17.5841108255988,13.4543167361568));
#141571=CARTESIAN_POINT('Ctrl Pts',(20.6545277281616,17.5160220847016,13.4587031981693));
#141572=CARTESIAN_POINT('Ctrl Pts',(20.5950264806455,17.450910248947,13.4630896601819));
#141573=CARTESIAN_POINT('Ctrl Pts',(20.5324338669329,17.3891230485379,13.4674761221944));
#141574=CARTESIAN_POINT('Ctrl Pts',(20.4698412532203,17.3273358481288,13.4718625842069));
#141575=CARTESIAN_POINT('Ctrl Pts',(20.4041577572906,17.2688736120053,13.4762490462195));
#141576=CARTESIAN_POINT('Ctrl Pts',(20.3357880909559,17.2140335727229,13.480635508232));
#141577=CARTESIAN_POINT('Ctrl Pts',(20.3218259507328,17.20283439099,13.4815312914205));
#141578=CARTESIAN_POINT('Ctrl Pts',(20.3077408086975,17.1917771969645,13.4824270746089));
#141579=CARTESIAN_POINT('Ctrl Pts',(20.2935357313021,17.1808649545432,13.4833228577973));
#141580=CARTESIAN_POINT('Origin',(18.734,19.211,-1.76670989022852));
#141581=CARTESIAN_POINT('',(20.2947698000194,17.1792870601113,14.3497865242445));
#141582=CARTESIAN_POINT('',(20.2923704939389,17.1824127799558,14.2834124336844));
#141583=CARTESIAN_POINT('',(20.2935357313021,17.1808649545432,-1.76670989022852));
#141584=CARTESIAN_POINT('',(16.1740010575059,19.2133268925441,13.8332901097715));
#141585=CARTESIAN_POINT('Ctrl Pts',(16.1735504167883,19.2133273021507,13.8332901097715));
#141586=CARTESIAN_POINT('Ctrl Pts',(16.1718448984259,19.397218647613,13.8424428639771));
#141587=CARTESIAN_POINT('Ctrl Pts',(16.2739023704358,20.430943821993,13.8939875537431));
#141588=CARTESIAN_POINT('Ctrl Pts',(17.6781137250704,22.0479692933859,13.9879241790696));
#141589=CARTESIAN_POINT('Ctrl Pts',(20.547911001461,21.6344309307215,14.1150999857511));
#141590=CARTESIAN_POINT('Ctrl Pts',(21.6914148573177,19.1334581591447,14.235720767476));
#141591=CARTESIAN_POINT('Ctrl Pts',(20.8607340381188,17.6225946302628,14.3139496136405));
#141592=CARTESIAN_POINT('Ctrl Pts',(20.2947698000194,17.1792870601114,14.3497865242445));
#141593=CARTESIAN_POINT('Ctrl Pts',(20.2935357313021,17.1808649545431,13.5498657053664));
#141594=CARTESIAN_POINT('Ctrl Pts',(20.2268456363114,17.1296340838212,13.554035809073));
#141595=CARTESIAN_POINT('Ctrl Pts',(20.1576422952453,17.0817034154883,13.5582059127796));
#141596=CARTESIAN_POINT('Ctrl Pts',(20.0862913115335,17.0373146021673,13.5623760164862));
#141597=CARTESIAN_POINT('Ctrl Pts',(20.014862512693,16.9928773785647,13.566550668093));
#141598=CARTESIAN_POINT('Ctrl Pts',(19.9412817874356,16.9519899633664,13.5707253196998));
#141599=CARTESIAN_POINT('Ctrl Pts',(19.8659411499047,16.914849039555,13.5748999713067));
#141600=CARTESIAN_POINT('Ctrl Pts',(19.7905547067899,16.8776855348131,13.5790771610172));
#141601=CARTESIAN_POINT('Ctrl Pts',(19.7134066434974,16.8442732382304,13.5832543507278));
#141602=CARTESIAN_POINT('Ctrl Pts',(19.6349086321998,16.8147605218952,13.5874315404384));
#141603=CARTESIAN_POINT('Ctrl Pts',(19.5562800602382,16.7851987189682,13.5916156777984));
#141604=CARTESIAN_POINT('Ctrl Pts',(19.47629749576,16.7595495841754,13.5957998151583));
#141605=CARTESIAN_POINT('Ctrl Pts',(19.3953870345571,16.7379114066577,13.5999839525183));
#141606=CARTESIAN_POINT('Ctrl Pts',(19.3540513033222,16.7268568424273,13.6021215546873));
#141607=CARTESIAN_POINT('Ctrl Pts',(19.3124735468993,16.7168483144191,13.6042591568563));
#141608=CARTESIAN_POINT('Ctrl Pts',(19.2707112385803,16.7078937205181,13.6063967590253));
#141609=CARTESIAN_POINT('Ctrl Pts',(19.1889560858867,16.6903639377749,13.6105813934184));
#141610=CARTESIAN_POINT('Ctrl Pts',(19.1061890642126,16.676811111084,13.6147660278114));
#141611=CARTESIAN_POINT('Ctrl Pts',(19.0228317972389,16.6673458975514,13.6189506622045));
#141612=CARTESIAN_POINT('Ctrl Pts',(18.9395931790174,16.6578941565786,13.6231293402884));
#141613=CARTESIAN_POINT('Ctrl Pts',(18.8557664374668,16.6525185234246,13.6273080183724));
#141614=CARTESIAN_POINT('Ctrl Pts',(18.771784329296,16.6512788541602,13.6314866964563));
#141615=CARTESIAN_POINT('Ctrl Pts',(18.6862969021931,16.6500169647151,13.6357402743417));
#141616=CARTESIAN_POINT('Ctrl Pts',(18.6006489552155,16.6530408729659,13.6399938522272));
#141617=CARTESIAN_POINT('Ctrl Pts',(18.5153034901262,16.6603585440974,13.6442474301126));
#141618=CARTESIAN_POINT('Ctrl Pts',(18.4316126134156,16.6675343478947,13.6484185440906));
#141619=CARTESIAN_POINT('Ctrl Pts',(18.3482130743119,16.6788388732104,13.6525896580685));
#141620=CARTESIAN_POINT('Ctrl Pts',(18.2655406685,16.6942270951215,13.6567607720465));
#141621=CARTESIAN_POINT('Ctrl Pts',(18.1828960042123,16.7096101533661,13.6609304863668));
#141622=CARTESIAN_POINT('Ctrl Pts',(18.1009784405238,16.7290741026091,13.6651002006872));
#141623=CARTESIAN_POINT('Ctrl Pts',(18.0202156389589,16.7525224455096,13.6692699150076));
#141624=CARTESIAN_POINT('Ctrl Pts',(17.9394557112813,16.7759699540174,13.6734394809516));
#141625=CARTESIAN_POINT('Ctrl Pts',(17.8598509055788,16.8034014451983,13.6776090468957));
#141626=CARTESIAN_POINT('Ctrl Pts',(17.7818144029991,16.8346703534939,13.6817786128397));
#141627=CARTESIAN_POINT('Ctrl Pts',(17.7010342332569,16.8670386380308,13.6860947755786));
#141628=CARTESIAN_POINT('Ctrl Pts',(17.6219351912177,16.9035190114424,13.6904109383175));
#141629=CARTESIAN_POINT('Ctrl Pts',(17.54495192229,16.9438950908936,13.6947271010565));
#141630=CARTESIAN_POINT('Ctrl Pts',(17.4704763752505,16.9829559238035,13.6989026652482));
#141631=CARTESIAN_POINT('Ctrl Pts',(17.3979812574156,17.0256622753739,13.7030782294398));
#141632=CARTESIAN_POINT('Ctrl Pts',(17.3278323932019,17.0717728821858,13.7072537936315));
#141633=CARTESIAN_POINT('Ctrl Pts',(17.25414047662,17.1202124261302,13.7116402556441));
#141634=CARTESIAN_POINT('Ctrl Pts',(17.1830385318337,17.1724088154588,13.7160267176566));
#141635=CARTESIAN_POINT('Ctrl Pts',(17.1149115381733,17.2280344045396,13.7204131796692));
#141636=CARTESIAN_POINT('Ctrl Pts',(17.046784544513,17.2836599936204,13.7247996416817));
#141637=CARTESIAN_POINT('Ctrl Pts',(16.9816328807926,17.3427143364292,13.7291861036942));
#141638=CARTESIAN_POINT('Ctrl Pts',(16.919795358022,17.4048268308312,13.7335725657068));
#141639=CARTESIAN_POINT('Ctrl Pts',(16.8612222805614,17.4636603639818,13.7377274633762));
#141640=CARTESIAN_POINT('Ctrl Pts',(16.8053896617353,17.5254713783546,13.7418823610455));
#141641=CARTESIAN_POINT('Ctrl Pts',(16.7526212754374,17.5899699725635,13.7460372587149));
#141642=CARTESIAN_POINT('Ctrl Pts',(16.70029462084,17.6539286398257,13.7501573751423));
#141643=CARTESIAN_POINT('Ctrl Pts',(16.650981430094,17.7205297194408,13.7542774915697));
#141644=CARTESIAN_POINT('Ctrl Pts',(16.6049624110077,17.7894519196813,13.7583976079971));
#141645=CARTESIAN_POINT('Ctrl Pts',(16.5589874739682,17.8583080987046,13.7625137777266));
#141646=CARTESIAN_POINT('Ctrl Pts',(16.5163007099123,17.9294805955777,13.7666299474561));
#141647=CARTESIAN_POINT('Ctrl Pts',(16.4771421768206,18.0026156381539,13.7707461171856));
#141648=CARTESIAN_POINT('Ctrl Pts',(16.4380086398887,18.0757039962642,13.7748596594307));
#141649=CARTESIAN_POINT('Ctrl Pts',(16.4023990866292,18.1507519968567,13.7789732016757));
#141650=CARTESIAN_POINT('Ctrl Pts',(16.3705090605921,18.2273788435904,13.7830867439208));
#141651=CARTESIAN_POINT('Ctrl Pts',(16.3380758082444,18.3053109799212,13.7872703577417));
#141652=CARTESIAN_POINT('Ctrl Pts',(16.3094902338593,18.384875816755,13.7914539715626));
#141653=CARTESIAN_POINT('Ctrl Pts',(16.2849076425234,18.4656499986249,13.7956375853835));
#141654=CARTESIAN_POINT('Ctrl Pts',(16.260736137924,18.5450734199358,13.7997512379815));
#141655=CARTESIAN_POINT('Ctrl Pts',(16.2404348481342,18.625665568199,13.8038648905794));
#141656=CARTESIAN_POINT('Ctrl Pts',(16.2241009663663,18.7070090864265,13.8079785431774));
#141657=CARTESIAN_POINT('Ctrl Pts',(16.2073503971231,18.7904277283583,13.8121971376098));
#141658=CARTESIAN_POINT('Ctrl Pts',(16.1947725425285,18.8746360871018,13.8164157320421));
#141659=CARTESIAN_POINT('Ctrl Pts',(16.1864159534739,18.9591756050623,13.8206343264745));
#141660=CARTESIAN_POINT('Ctrl Pts',(16.1780593644194,19.0437151230227,13.8248529209068));
#141661=CARTESIAN_POINT('Ctrl Pts',(16.1739240322153,19.1285852645551,13.8290715153392));
#141662=CARTESIAN_POINT('Ctrl Pts',(16.1740010575059,19.2133268925441,13.8332901097715));
#141663=CARTESIAN_POINT('',(16.1740010826188,19.2086456408846,13.7667098774927));
#141664=CARTESIAN_POINT('Ctrl Pts',(20.2935357313021,17.1808649545432,13.4833228577973));
#141665=CARTESIAN_POINT('Ctrl Pts',(20.2271990472176,17.1299055716403,13.4875061005018));
#141666=CARTESIAN_POINT('Ctrl Pts',(20.1582439195132,17.0821103150656,13.4916893432062));
#141667=CARTESIAN_POINT('Ctrl Pts',(20.0870050548683,17.037758798131,13.4958725859106));
#141668=CARTESIAN_POINT('Ctrl Pts',(20.0158625393595,16.9934672657339,13.5000501708631));
#141669=CARTESIAN_POINT('Ctrl Pts',(19.9424428099246,16.952610462243,13.5042277558156));
#141670=CARTESIAN_POINT('Ctrl Pts',(19.8671122176929,16.9154267160217,13.5084053407681));
#141671=CARTESIAN_POINT('Ctrl Pts',(19.7918615726562,16.8782824323364,13.5125784921142));
#141672=CARTESIAN_POINT('Ctrl Pts',(19.7147045060799,16.8448036608316,13.5167516434603));
#141673=CARTESIAN_POINT('Ctrl Pts',(19.6360336298753,16.8151837861443,13.5209247948064));
#141674=CARTESIAN_POINT('Ctrl Pts',(19.5574081539594,16.7855810048329,13.5250955378626));
#141675=CARTESIAN_POINT('Ctrl Pts',(19.4772710323891,16.7598328607242,13.5292662809187));
#141676=CARTESIAN_POINT('Ctrl Pts',(19.3960355713781,16.7380849383309,13.5334370239749));
#141677=CARTESIAN_POINT('Ctrl Pts',(19.3148226216747,16.7163430425441,13.5376066112689));
#141678=CARTESIAN_POINT('Ctrl Pts',(19.2325123812022,16.6985992855769,13.5417761985628));
#141679=CARTESIAN_POINT('Ctrl Pts',(19.1495327464081,16.6849492212819,13.5459457858567));
#141680=CARTESIAN_POINT('Ctrl Pts',(19.0665512144905,16.671298844912,13.5501154684779));
#141681=CARTESIAN_POINT('Ctrl Pts',(18.9829007120166,16.6617424204531,13.5542851510991));
#141682=CARTESIAN_POINT('Ctrl Pts',(18.8990173854919,16.6563240396314,13.5584548337203));
#141683=CARTESIAN_POINT('Ctrl Pts',(18.81504898099,16.6509001632612,13.562628745408));
#141684=CARTESIAN_POINT('Ctrl Pts',(18.7308477408885,16.6496227436427,13.5668026570956));
#141685=CARTESIAN_POINT('Ctrl Pts',(18.6468524989643,16.6524837672856,13.5709765687833));
#141686=CARTESIAN_POINT('Ctrl Pts',(18.5628158254364,16.6553462021608,13.5751525393001));
#141687=CARTESIAN_POINT('Ctrl Pts',(18.4789858114393,16.6623511081852,13.5793285098169));
#141688=CARTESIAN_POINT('Ctrl Pts',(18.395796391128,16.6734385093271,13.5835044803338));
#141689=CARTESIAN_POINT('Ctrl Pts',(18.3124575762843,16.68454582162,13.5876879502076));
#141690=CARTESIAN_POINT('Ctrl Pts',(18.2297621072741,16.6997501950311,13.5918714200815));
#141691=CARTESIAN_POINT('Ctrl Pts',(18.1481338641761,16.7189404359256,13.5960548899553));
#141692=CARTESIAN_POINT('Ctrl Pts',(18.0716697213006,16.7369166322258,13.5999736982747));
#141693=CARTESIAN_POINT('Ctrl Pts',(17.9961422105312,16.7583897434859,13.6038925065941));
#141694=CARTESIAN_POINT('Ctrl Pts',(17.921884774769,16.783229652346,13.6078113149135));
#141695=CARTESIAN_POINT('Ctrl Pts',(17.842590205016,16.809754536562,13.6119959493065));
#141696=CARTESIAN_POINT('Ctrl Pts',(17.7644489508447,16.8402176845382,13.6161805836996));
#141697=CARTESIAN_POINT('Ctrl Pts',(17.6878802554244,16.8744997367838,13.6203652180926));
#141698=CARTESIAN_POINT('Ctrl Pts',(17.6114205460648,16.9087329927714,13.6245438961766));
#141699=CARTESIAN_POINT('Ctrl Pts',(17.5365293656819,16.9467741695629,13.6287225742605));
#141700=CARTESIAN_POINT('Ctrl Pts',(17.4636096823066,16.9884545132415,13.6329012523445));
#141701=CARTESIAN_POINT('Ctrl Pts',(17.3893829660133,17.0308819471252,13.6371548302299));
#141702=CARTESIAN_POINT('Ctrl Pts',(17.3171995773181,17.0770801423178,13.6414084081153));
#141703=CARTESIAN_POINT('Ctrl Pts',(17.2474621052951,17.126820284235,13.6456619860008));
#141704=CARTESIAN_POINT('Ctrl Pts',(17.1790766302487,17.1755961164412,13.6498330999787));
#141705=CARTESIAN_POINT('Ctrl Pts',(17.1130434722311,17.2277775063953,13.6540042139567));
#141706=CARTESIAN_POINT('Ctrl Pts',(17.0497148300456,17.2831038756531,13.6581753279346));
#141707=CARTESIAN_POINT('Ctrl Pts',(16.9864074383976,17.3384116796135,13.662345042255));
#141708=CARTESIAN_POINT('Ctrl Pts',(16.9258031063752,17.3968620645643,13.6665147565754));
#141709=CARTESIAN_POINT('Ctrl Pts',(16.8682208314236,17.4581542868505,13.6706844708957));
#141710=CARTESIAN_POINT('Ctrl Pts',(16.8106406054966,17.5194443280964,13.6748540368398));
#141711=CARTESIAN_POINT('Ctrl Pts',(16.7560825371937,17.5835756697509,13.6790236027838));
#141712=CARTESIAN_POINT('Ctrl Pts',(16.7048276747609,17.650211841894,13.6831931687278));
#141713=CARTESIAN_POINT('Ctrl Pts',(16.6517707545947,17.7191908596451,13.6875093314668));
#141714=CARTESIAN_POINT('Ctrl Pts',(16.6022539651132,17.7908537067502,13.6918254942057));
#141715=CARTESIAN_POINT('Ctrl Pts',(16.5565412927829,17.8647928917271,13.6961416569446));
#141716=CARTESIAN_POINT('Ctrl Pts',(16.5123177059456,17.9363235155305,13.7003172211363));
#141717=CARTESIAN_POINT('Ctrl Pts',(16.4716543903427,18.0099840160617,13.704492785328));
#141718=CARTESIAN_POINT('Ctrl Pts',(16.4347434295141,18.0853805158593,13.7086683495197));
#141719=CARTESIAN_POINT('Ctrl Pts',(16.3959681838015,18.1645851136235,13.7130548115322));
#141720=CARTESIAN_POINT('Ctrl Pts',(16.3613345469612,18.2457051531361,13.7174412735447));
#141721=CARTESIAN_POINT('Ctrl Pts',(16.3310071212994,18.3282626523624,13.7218277355573));
#141722=CARTESIAN_POINT('Ctrl Pts',(16.3006796956376,18.4108201515888,13.7262141975698));
#141723=CARTESIAN_POINT('Ctrl Pts',(16.2746585801944,18.494814533789,13.7306006595824));
#141724=CARTESIAN_POINT('Ctrl Pts',(16.253046772176,18.5797543415202,13.7349871215949));
#141725=CARTESIAN_POINT('Ctrl Pts',(16.2263033450825,18.6848626949471,13.7404151277539));
#141726=CARTESIAN_POINT('Ctrl Pts',(16.2062281520531,18.7917315462651,13.7458431339129));
#141727=CARTESIAN_POINT('Ctrl Pts',(16.1930065418683,18.8996284442475,13.7512711400719));
#141728=CARTESIAN_POINT('Ctrl Pts',(16.180471247327,19.0019245622985,13.7564173858788));
#141729=CARTESIAN_POINT('Ctrl Pts',(16.1740962693074,19.1051449394228,13.7615636316857));
#141730=CARTESIAN_POINT('Ctrl Pts',(16.1740010826188,19.2086456408846,13.7667098774927));
#141731=CARTESIAN_POINT('Ctrl Pts',(16.1744182524956,19.2086462806443,13.7667098902285));
#141732=CARTESIAN_POINT('Ctrl Pts',(16.1802301046829,19.8484613837252,13.7985275695778));
#141733=CARTESIAN_POINT('Ctrl Pts',(16.7471749375075,21.3499116609599,13.8727371844876));
#141734=CARTESIAN_POINT('Ctrl Pts',(19.2691669576991,22.1904107317588,13.9893387349578));
#141735=CARTESIAN_POINT('Ctrl Pts',(21.528888647397,20.3737078006893,14.1165145416392));
#141736=CARTESIAN_POINT('Ctrl Pts',(21.294251524494,18.1512291001575,14.2145391078814));
#141737=CARTESIAN_POINT('Ctrl Pts',(20.5052428603892,17.3430212386448,14.2701717385632));
#141738=CARTESIAN_POINT('Ctrl Pts',(20.2923704939387,17.1824127799556,14.2834124336845));
#141739=CARTESIAN_POINT('Origin',(18.734,19.211,-1.76670989022852));
#141740=CARTESIAN_POINT('',(20.2935357313021,17.1808649545431,15.149955387129));
#141741=CARTESIAN_POINT('',(20.2935357313021,17.1808649545432,15.0832685864905));
#141742=CARTESIAN_POINT('',(20.2935357313021,17.1808649545432,-1.76670989022852));
#141743=CARTESIAN_POINT('',(16.1738766799073,19.2098698167329,14.6332901097715));
#141744=CARTESIAN_POINT('Ctrl Pts',(16.1740002494514,19.2098698712835,14.6332901097715));
#141745=CARTESIAN_POINT('Ctrl Pts',(16.1739637014967,19.2926593390013,14.6374299052976));
#141746=CARTESIAN_POINT('Ctrl Pts',(16.1779474618949,19.3756125071059,14.6415697008237));
#141747=CARTESIAN_POINT('Ctrl Pts',(16.1859729132155,19.4583013647604,14.6457094963498));
#141748=CARTESIAN_POINT('Ctrl Pts',(16.1939875490477,19.5408787868903,14.6498437128862));
#141749=CARTESIAN_POINT('Ctrl Pts',(16.2060330170348,19.6231921412973,14.6539779294227));
#141750=CARTESIAN_POINT('Ctrl Pts',(16.2220786798975,19.7048130026784,14.6581121459591));
#141751=CARTESIAN_POINT('Ctrl Pts',(16.2381078732804,19.7863500873324,14.6622421190812));
#141752=CARTESIAN_POINT('Ctrl Pts',(16.2581290152452,19.8671956313601,14.6663720922033));
#141753=CARTESIAN_POINT('Ctrl Pts',(16.2820597821147,19.9469274202778,14.6705020653254));
#141754=CARTESIAN_POINT('Ctrl Pts',(16.3059775967094,20.0266160552067,14.6746298031431));
#141755=CARTESIAN_POINT('Ctrl Pts',(16.3338007023326,20.1051916814476,14.6787575409609));
#141756=CARTESIAN_POINT('Ctrl Pts',(16.3653962152437,20.1822446194642,14.6828852787787));
#141757=CARTESIAN_POINT('Ctrl Pts',(16.3969845852851,20.2592801379472,14.6870120834293));
#141758=CARTESIAN_POINT('Ctrl Pts',(16.4323434905921,20.3347932165774,14.69113888808));
#141759=CARTESIAN_POINT('Ctrl Pts',(16.4712914723381,20.4083930511099,14.6952656927307));
#141760=CARTESIAN_POINT('Ctrl Pts',(16.5102429241535,20.4819994430175,14.6993928650588));
#141761=CARTESIAN_POINT('Ctrl Pts',(16.5527838651363,20.5536918375771,14.703520037387));
#141762=CARTESIAN_POINT('Ctrl Pts',(16.5986870593961,20.6231043324377,14.7076472097152));
#141763=CARTESIAN_POINT('Ctrl Pts',(16.6446377721104,20.6925886823084,14.7117786544444));
#141764=CARTESIAN_POINT('Ctrl Pts',(16.6939574240325,20.7597880294055,14.7159100991735));
#141765=CARTESIAN_POINT('Ctrl Pts',(16.7463760416131,20.8243663564257,14.7200415439027));
#141766=CARTESIAN_POINT('Ctrl Pts',(16.7988250781885,20.8889821588294,14.7241753861463));
#141767=CARTESIAN_POINT('Ctrl Pts',(16.8543763437708,20.9509735655353,14.7283092283899));
#141768=CARTESIAN_POINT('Ctrl Pts',(16.9127219511763,21.0100403744422,14.7324430706336));
#141769=CARTESIAN_POINT('Ctrl Pts',(16.9711635405887,21.0692043517755,14.7365837132945));
#141770=CARTESIAN_POINT('Ctrl Pts',(17.0324082986529,21.1254338132414,14.7407243559553));
#141771=CARTESIAN_POINT('Ctrl Pts',(17.0961145829399,21.1784682616454,14.7448649986162));
#141772=CARTESIAN_POINT('Ctrl Pts',(17.1274705472745,21.2045715933853,14.7469030054636));
#141773=CARTESIAN_POINT('Ctrl Pts',(17.1594223751536,21.2299015689542,14.7489410123109));
#141774=CARTESIAN_POINT('Ctrl Pts',(17.1919269101815,21.2544310817,14.7509790191583));
#141775=CARTESIAN_POINT('Ctrl Pts',(17.2586683911457,21.3047974692387,14.7551636535514));
#141776=CARTESIAN_POINT('Ctrl Pts',(17.3280042311,21.3519843348469,14.7593482879444));
#141777=CARTESIAN_POINT('Ctrl Pts',(17.3995987737075,21.395713566413,14.7635329223375));
#141778=CARTESIAN_POINT('Ctrl Pts',(17.4710914103449,21.4393805548304,14.7677116004214));
#141779=CARTESIAN_POINT('Ctrl Pts',(17.5448359744303,21.4795994471399,14.7718902785053));
#141780=CARTESIAN_POINT('Ctrl Pts',(17.6204652949927,21.5161335017183,14.7760689565893));
#141781=CARTESIAN_POINT('Ctrl Pts',(17.6974502167725,21.5533224029686,14.7803225344747));
#141782=CARTESIAN_POINT('Ctrl Pts',(17.7763877432988,21.5866927752842,14.7845761123601));
#141783=CARTESIAN_POINT('Ctrl Pts',(17.8568613993343,21.616042177431,14.7888296902455));
#141784=CARTESIAN_POINT('Ctrl Pts',(17.9357749165162,21.6448225841466,14.7930008042235));
#141785=CARTESIAN_POINT('Ctrl Pts',(18.0161650808992,21.6697363732161,14.7971719182015));
#141786=CARTESIAN_POINT('Ctrl Pts',(18.0976177441658,21.6906406240541,14.8013430321794));
#141787=CARTESIAN_POINT('Ctrl Pts',(18.1790430752045,21.7115378602688,14.8055127464998));
#141788=CARTESIAN_POINT('Ctrl Pts',(18.2615297518276,21.7284281160528,14.8096824608201));
#141789=CARTESIAN_POINT('Ctrl Pts',(18.34464929881,21.7412185738554,14.8138521751405));
#141790=CARTESIAN_POINT('Ctrl Pts',(18.4277658880425,21.7540085765186,14.8180217410846));
#141791=CARTESIAN_POINT('Ctrl Pts',(18.5115148480474,21.7626990021399,14.8221913070286));
#141792=CARTESIAN_POINT('Ctrl Pts',(18.5954597232798,21.7672485387235,14.8263608729727));
#141793=CARTESIAN_POINT('Ctrl Pts',(18.682355996768,21.7719580314011,14.8306770357116));
#141794=CARTESIAN_POINT('Ctrl Pts',(18.7694616919209,21.7722300013651,14.8349931984505));
#141795=CARTESIAN_POINT('Ctrl Pts',(18.8562914526108,21.7680773943349,14.8393093611894));
#141796=CARTESIAN_POINT('Ctrl Pts',(18.9402927429791,21.7640600580418,14.8434849253811));
#141797=CARTESIAN_POINT('Ctrl Pts',(19.0240353356991,21.7559020718403,14.8476604895728));
#141798=CARTESIAN_POINT('Ctrl Pts',(19.1070857885135,21.7436679597628,14.8518360537644));
#141799=CARTESIAN_POINT('Ctrl Pts',(19.1943309222658,21.7308159317682,14.856222515777));
#141800=CARTESIAN_POINT('Ctrl Pts',(19.2808115861344,21.7134653009972,14.8606089777895));
#141801=CARTESIAN_POINT('Ctrl Pts',(19.3660405469232,21.6917508434031,14.864995439802));
#141802=CARTESIAN_POINT('Ctrl Pts',(19.4512695077121,21.6700363858089,14.8693819018146));
#141803=CARTESIAN_POINT('Ctrl Pts',(19.5352462338657,21.6439583461085,14.8737683638271));
#141804=CARTESIAN_POINT('Ctrl Pts',(19.6175072439392,21.6137099179691,14.8781548258397));
#141805=CARTESIAN_POINT('Ctrl Pts',(19.6959833029991,21.5848532648472,14.8823394602327));
#141806=CARTESIAN_POINT('Ctrl Pts',(19.7731901646012,21.5520941514644,14.8865240946257));
#141807=CARTESIAN_POINT('Ctrl Pts',(19.8487122960628,21.5155642748698,14.8907087290188));
#141808=CARTESIAN_POINT('Ctrl Pts',(19.924126931118,21.4790863940332,14.8948874071027));
#141809=CARTESIAN_POINT('Ctrl Pts',(19.997861188636,21.4388486095631,14.8990660851867));
#141810=CARTESIAN_POINT('Ctrl Pts',(20.069517263694,21.3950315103897,14.9032447632706));
#141811=CARTESIAN_POINT('Ctrl Pts',(20.1424577223992,21.3504290212044,14.907498341156));
#141812=CARTESIAN_POINT('Ctrl Pts',(20.2132443104809,21.3021178031455,14.9117519190415));
#141813=CARTESIAN_POINT('Ctrl Pts',(20.2814813767513,21.2503384683784,14.9160054969269));
#141814=CARTESIAN_POINT('Ctrl Pts',(20.3483955343384,21.1995629770548,14.9201766109049));
#141815=CARTESIAN_POINT('Ctrl Pts',(20.4128577595137,21.145452932324,14.9243477248828));
#141816=CARTESIAN_POINT('Ctrl Pts',(20.4745237080533,21.0882792071784,14.9285188388608));
#141817=CARTESIAN_POINT('Ctrl Pts',(20.5361689639883,21.0311246672285,14.9326885531811));
#141818=CARTESIAN_POINT('Ctrl Pts',(20.5950194697343,20.9709088010949,14.9368582675015));
#141819=CARTESIAN_POINT('Ctrl Pts',(20.6507652549071,20.9079416482546,14.9410279818219));
#141820=CARTESIAN_POINT('Ctrl Pts',(20.7065090564057,20.8449767360557,14.9451975477659));
#141821=CARTESIAN_POINT('Ctrl Pts',(20.7591480526894,20.7792610768138,14.9493671137099));
#141822=CARTESIAN_POINT('Ctrl Pts',(20.8084112617993,20.711139299172,14.953536679654));
#141823=CARTESIAN_POINT('Ctrl Pts',(20.8594065045688,20.6406224438655,14.9578528423929));
#141824=CARTESIAN_POINT('Ctrl Pts',(20.9067838489647,20.5675275512001,14.9621690051318));
#141825=CARTESIAN_POINT('Ctrl Pts',(20.9502914662215,20.4922697361422,14.9664851678708));
#141826=CARTESIAN_POINT('Ctrl Pts',(20.9923818274223,20.4194634364942,14.9706607320624));
#141827=CARTESIAN_POINT('Ctrl Pts',(21.0308505291915,20.3446334053669,14.9748362962541));
#141828=CARTESIAN_POINT('Ctrl Pts',(21.0655172119567,20.2681790247398,14.9790118604458));
#141829=CARTESIAN_POINT('Ctrl Pts',(21.1019348264562,20.1878631151,14.9833983224583));
#141830=CARTESIAN_POINT('Ctrl Pts',(21.1341560348913,20.1057549952925,14.9877847844709));
#141831=CARTESIAN_POINT('Ctrl Pts',(21.162030432422,20.0223373029958,14.9921712464835));
#141832=CARTESIAN_POINT('Ctrl Pts',(21.1899048299528,19.938919610699,14.996557708496));
#141833=CARTESIAN_POINT('Ctrl Pts',(21.2134323346265,19.8541929253279,15.0009441705086));
#141834=CARTESIAN_POINT('Ctrl Pts',(21.2325245180281,19.7686515334979,15.0053306325211));
#141835=CARTESIAN_POINT('Ctrl Pts',(21.2507382417699,19.6870460279089,15.0095152669142));
#141836=CARTESIAN_POINT('Ctrl Pts',(21.2649836214983,19.6043953888038,15.0136999013072));
#141837=CARTESIAN_POINT('Ctrl Pts',(21.2751464736302,19.5211202985242,15.0178845357003));
#141838=CARTESIAN_POINT('Ctrl Pts',(21.2852948602001,19.4379637400282,15.0220632137842));
#141839=CARTESIAN_POINT('Ctrl Pts',(21.2913722063418,19.3541849485909,15.0262418918681));
#141840=CARTESIAN_POINT('Ctrl Pts',(21.2933150345072,19.2702161645612,15.0304205699521));
#141841=CARTESIAN_POINT('Ctrl Pts',(21.2952926864712,19.1847423004251,15.0346741478375));
#141842=CARTESIAN_POINT('Ctrl Pts',(21.2929860350544,19.0990720360282,15.038927725723));
#141843=CARTESIAN_POINT('Ctrl Pts',(21.2863832385264,19.0136682902081,15.0431813036084));
#141844=CARTESIAN_POINT('Ctrl Pts',(21.2799084500935,18.9299202626523,15.0473524175864));
#141845=CARTESIAN_POINT('Ctrl Pts',(21.2693026454397,18.8464289917135,15.0515235315643));
#141846=CARTESIAN_POINT('Ctrl Pts',(21.2546071988876,18.7636306348037,15.0556946455423));
#141847=CARTESIAN_POINT('Ctrl Pts',(21.2399166835345,18.6808600616823,15.0598643598626));
#141848=CARTESIAN_POINT('Ctrl Pts',(21.2211393320557,18.5987823933904,15.064034074183));
#141849=CARTESIAN_POINT('Ctrl Pts',(21.1983680574965,18.5178260844557,15.0682037885034));
#141850=CARTESIAN_POINT('Ctrl Pts',(21.1755975932369,18.436872656294,15.0723733544475));
#141851=CARTESIAN_POINT('Ctrl Pts',(21.1488336138538,18.3570409507695,15.0765429203915));
#141852=CARTESIAN_POINT('Ctrl Pts',(21.1182192201025,18.2787453617742,15.0807124863355));
#141853=CARTESIAN_POINT('Ctrl Pts',(21.0865284620339,18.1976969964578,15.0850286490745));
#141854=CARTESIAN_POINT('Ctrl Pts',(21.0507116827589,18.1182952684028,15.0893448118134));
#141855=CARTESIAN_POINT('Ctrl Pts',(21.0109816181366,18.0409766196062,15.0936609745523));
#141856=CARTESIAN_POINT('Ctrl Pts',(20.9725457561904,17.9661766176617,15.097836538744));
#141857=CARTESIAN_POINT('Ctrl Pts',(20.9304479207725,17.8933264506923,15.1020121029357));
#141858=CARTESIAN_POINT('Ctrl Pts',(20.8849263037083,17.8227939504469,15.1061876671273));
#141859=CARTESIAN_POINT('Ctrl Pts',(20.8371054979835,17.7486990212892,15.1105741291399));
#141860=CARTESIAN_POINT('Ctrl Pts',(20.7855062921195,17.6771625161641,15.1149605911524));
#141861=CARTESIAN_POINT('Ctrl Pts',(20.7304530967377,17.6085721443614,15.119347053165));
#141862=CARTESIAN_POINT('Ctrl Pts',(20.6753999013559,17.5399817725587,15.1237335151775));
#141863=CARTESIAN_POINT('Ctrl Pts',(20.616893159293,17.474337916614,15.12811997719));
#141864=CARTESIAN_POINT('Ctrl Pts',(20.5553006227462,17.4119824788001,15.1325064392026));
#141865=CARTESIAN_POINT('Ctrl Pts',(20.4965457256996,17.3524998282314,15.1366908118295));
#141866=CARTESIAN_POINT('Ctrl Pts',(20.434764426497,17.2957878690111,15.1408751844563));
#141867=CARTESIAN_POINT('Ctrl Pts',(20.3702485909646,17.2421702591219,15.1450595570832));
#141868=CARTESIAN_POINT('Ctrl Pts',(20.3450868288406,17.2212589040327,15.1466915004318));
#141869=CARTESIAN_POINT('Ctrl Pts',(20.3195095624847,17.2008178724038,15.1483234437804));
#141870=CARTESIAN_POINT('Ctrl Pts',(20.2935357313021,17.1808649545431,15.149955387129));
#141871=CARTESIAN_POINT('Ctrl Pts',(20.2947698000194,17.1792870601114,14.3497865242445));
#141872=CARTESIAN_POINT('Ctrl Pts',(20.1912477708408,17.0982004894008,14.356341549201));
#141873=CARTESIAN_POINT('Ctrl Pts',(19.3719149925772,16.5548827574419,14.405288509718));
#141874=CARTESIAN_POINT('Ctrl Pts',(17.2895133755746,16.5507840333809,14.4966274057954));
#141875=CARTESIAN_POINT('Ctrl Pts',(16.200898327955,18.2345794040693,14.5845735760146));
#141876=CARTESIAN_POINT('Ctrl Pts',(16.1700292343928,19.1465375881033,14.6301278106733));
#141877=CARTESIAN_POINT('Ctrl Pts',(16.1703790132248,19.209868272665,14.6332901097715));
#141878=CARTESIAN_POINT('',(16.17436451349,19.211560173865,14.5667099150528));
#141879=CARTESIAN_POINT('Ctrl Pts',(20.2923704939387,17.1824127799556,14.2834124336845));
#141880=CARTESIAN_POINT('Ctrl Pts',(19.8237022344235,16.8288108162419,14.3125636741237));
#141881=CARTESIAN_POINT('Ctrl Pts',(18.3750627724065,16.3386617668037,14.3841068501234));
#141882=CARTESIAN_POINT('Ctrl Pts',(16.5197423492181,17.430869440195,14.478539335638));
#141883=CARTESIAN_POINT('Ctrl Pts',(16.1790023518676,18.7496082788979,14.5438205807135));
#141884=CARTESIAN_POINT('Ctrl Pts',(16.1781028428963,19.2115588546613,14.5667098902285));
#141885=CARTESIAN_POINT('Ctrl Pts',(16.1740000613162,19.211560302475,14.5667099174729));
#141886=CARTESIAN_POINT('Ctrl Pts',(16.1740197372987,19.30145909156,14.5711571992719));
#141887=CARTESIAN_POINT('Ctrl Pts',(16.1787790795977,19.3912344818004,14.5756044810709));
#141888=CARTESIAN_POINT('Ctrl Pts',(16.1882138900509,19.4803939167657,14.5800517628699));
#141889=CARTESIAN_POINT('Ctrl Pts',(16.1976832329532,19.5698796851174,14.5845153222118));
#141890=CARTESIAN_POINT('Ctrl Pts',(16.2118622325346,19.6587446305158,14.5889788815537));
#141891=CARTESIAN_POINT('Ctrl Pts',(16.2306352202496,19.7465042292131,14.5934424408955));
#141892=CARTESIAN_POINT('Ctrl Pts',(16.2494446598929,19.8344342326776,14.59791466723));
#141893=CARTESIAN_POINT('Ctrl Pts',(16.2728657964751,19.9212542602436,14.6023868935645));
#141894=CARTESIAN_POINT('Ctrl Pts',(16.3007333122769,20.0064955854165,14.606859119899));
#141895=CARTESIAN_POINT('Ctrl Pts',(16.3286838403156,20.0919908289195,14.6113446681784));
#141896=CARTESIAN_POINT('Ctrl Pts',(16.3611071025133,20.175897631469,14.6158302164578));
#141897=CARTESIAN_POINT('Ctrl Pts',(16.3977895032108,20.2577666954446,14.6203157647373));
#141898=CARTESIAN_POINT('Ctrl Pts',(16.4111522146037,20.2875900617759,14.6219497659465));
#141899=CARTESIAN_POINT('Ctrl Pts',(16.4250796827617,20.3171432681483,14.6235837671557));
#141900=CARTESIAN_POINT('Ctrl Pts',(16.4395601204677,20.3464054955,14.625217768365));
#141901=CARTESIAN_POINT('Ctrl Pts',(16.4766441429939,20.4213452949944,14.629402402758));
#141902=CARTESIAN_POINT('Ctrl Pts',(16.5174725051856,20.4946058152549,14.633587037151));
#141903=CARTESIAN_POINT('Ctrl Pts',(16.5618698248528,20.5657879916116,14.6377716715441));
#141904=CARTESIAN_POINT('Ctrl Pts',(16.6062039504308,20.636868848951,14.641950349628));
#141905=CARTESIAN_POINT('Ctrl Pts',(16.6540967016935,20.7058768514384,14.646129027712));
#141906=CARTESIAN_POINT('Ctrl Pts',(16.7053259809371,20.7724357893872,14.6503077057959));
#141907=CARTESIAN_POINT('Ctrl Pts',(16.7574735081934,20.8401877484638,14.6545612836814));
#141908=CARTESIAN_POINT('Ctrl Pts',(16.8130781406444,20.9054015483267,14.6588148615668));
#141909=CARTESIAN_POINT('Ctrl Pts',(16.8718583319471,20.9677095400496,14.6630684394523));
#141910=CARTESIAN_POINT('Ctrl Pts',(16.9294989545412,21.0288095697688,14.6672395534302));
#141911=CARTESIAN_POINT('Ctrl Pts',(16.9901927757377,21.0871151053885,14.6714106674082));
#141912=CARTESIAN_POINT('Ctrl Pts',(17.0536336491124,21.1423127470207,14.6755817813861));
#141913=CARTESIAN_POINT('Ctrl Pts',(17.1170532342894,21.1974918665512,14.6797514957065));
#141914=CARTESIAN_POINT('Ctrl Pts',(17.1832176941668,21.249564861567,14.6839212100268));
#141915=CARTESIAN_POINT('Ctrl Pts',(17.2517856166925,21.2982566976576,14.6880909243472));
#141916=CARTESIAN_POINT('Ctrl Pts',(17.3203510992774,21.3469468010837,14.6922604902913));
#141917=CARTESIAN_POINT('Ctrl Pts',(17.3913194988898,21.3922557191442,14.6964300562353));
#141918=CARTESIAN_POINT('Ctrl Pts',(17.4643191824367,21.4339508814888,14.7005996221793));
#141919=CARTESIAN_POINT('Ctrl Pts',(17.5398854448023,21.4771119943049,14.7049157849183));
#141920=CARTESIAN_POINT('Ctrl Pts',(17.6176280306767,21.5164002423865,14.7092319476572));
#141921=CARTESIAN_POINT('Ctrl Pts',(17.6971072733111,21.5516096371116,14.7135481103961));
#141922=CARTESIAN_POINT('Ctrl Pts',(17.7739974879763,21.5856720895068,14.7177236745878));
#141923=CARTESIAN_POINT('Ctrl Pts',(17.8525124972024,21.6159172197027,14.7218992387795));
#141924=CARTESIAN_POINT('Ctrl Pts',(17.9322359204944,21.6422084157502,14.7260748029711));
#141925=CARTESIAN_POINT('Ctrl Pts',(18.0159859843726,21.6698275176087,14.7304612649837));
#141926=CARTESIAN_POINT('Ctrl Pts',(18.1010691812453,21.6930826078308,14.7348477269962));
#141927=CARTESIAN_POINT('Ctrl Pts',(18.1869895560291,21.7118757614457,14.7392341890088));
#141928=CARTESIAN_POINT('Ctrl Pts',(18.2729099308129,21.7306689150606,14.7436206510213));
#141929=CARTESIAN_POINT('Ctrl Pts',(18.3596668986516,21.7450001125529,14.7480071130339));
#141930=CARTESIAN_POINT('Ctrl Pts',(18.4467595506039,21.7548342957494,14.7523935750464));
#141931=CARTESIAN_POINT('Ctrl Pts',(18.5298449405376,21.7642159935992,14.7565782094394));
#141932=CARTESIAN_POINT('Ctrl Pts',(18.6135450624313,21.7695403323457,14.7607628438325));
#141933=CARTESIAN_POINT('Ctrl Pts',(18.6974294349979,21.7707387745189,14.7649474782255));
#141934=CARTESIAN_POINT('Ctrl Pts',(18.781194408543,21.7719355108579,14.7691261563095));
#141935=CARTESIAN_POINT('Ctrl Pts',(18.8651426557824,21.7690180091444,14.7733048343934));
#141936=CARTESIAN_POINT('Ctrl Pts',(18.9488376266316,21.7619693832313,14.7774835124774));
#141937=CARTESIAN_POINT('Ctrl Pts',(19.0340327696827,21.7547944157644,14.7817370903628));
#141938=CARTESIAN_POINT('Ctrl Pts',(19.1189649879803,21.7433387124852,14.7859906682483));
#141939=CARTESIAN_POINT('Ctrl Pts',(19.2031727512633,21.7276400079217,14.7902442461337));
#141940=CARTESIAN_POINT('Ctrl Pts',(19.2857479827372,21.7122456533796,14.7944153601116));
#141941=CARTESIAN_POINT('Ctrl Pts',(19.3676261254066,21.6927714353378,14.7985864740896));
#141942=CARTESIAN_POINT('Ctrl Pts',(19.4483779483096,21.6693051370749,14.8027575880675));
#141943=CARTESIAN_POINT('Ctrl Pts',(19.5291026741586,21.6458467131551,14.8069273023879));
#141944=CARTESIAN_POINT('Ctrl Pts',(19.6087013894602,21.6183989977105,14.8110970167083));
#141945=CARTESIAN_POINT('Ctrl Pts',(19.686758033932,21.5871001933374,14.8152667310287));
#141946=CARTESIAN_POINT('Ctrl Pts',(19.7648119008134,21.55580250271,14.8194362969727));
#141947=CARTESIAN_POINT('Ctrl Pts',(19.8413233792987,21.5206541676233,14.8236058629168));
#141948=CARTESIAN_POINT('Ctrl Pts',(19.9158957565834,21.4818417867765,14.8277754288608));
#141949=CARTESIAN_POINT('Ctrl Pts',(19.9930900066584,21.4416648104994,14.8320915915997));
#141950=CARTESIAN_POINT('Ctrl Pts',(20.068205793024,21.397561582336,14.8364077543386));
#141951=CARTESIAN_POINT('Ctrl Pts',(20.1408319285751,21.349790294709,14.8407239170776));
#141952=CARTESIAN_POINT('Ctrl Pts',(20.2110922753996,21.3035751517518,14.8448994812692));
#141953=CARTESIAN_POINT('Ctrl Pts',(20.2790223288379,21.253927569593,14.8490750454609));
#141954=CARTESIAN_POINT('Ctrl Pts',(20.3442818409956,21.2011237128781,14.8532506096526));
#141955=CARTESIAN_POINT('Ctrl Pts',(20.4128374559725,21.1456528588899,14.8576370716651));
#141956=CARTESIAN_POINT('Ctrl Pts',(20.4784452273881,21.0866988942974,14.8620235336777));
#141957=CARTESIAN_POINT('Ctrl Pts',(20.5407543647588,21.0246258339098,14.8664099956902));
#141958=CARTESIAN_POINT('Ctrl Pts',(20.6030635021294,20.9625527735222,14.8707964577027));
#141959=CARTESIAN_POINT('Ctrl Pts',(20.6620736724742,20.8973610985477,14.8751829197153));
#141960=CARTESIAN_POINT('Ctrl Pts',(20.7174842649081,20.8294530178111,14.8795693817278));
#141961=CARTESIAN_POINT('Ctrl Pts',(20.770345333846,20.764669488533,14.8837540161209));
#141962=CARTESIAN_POINT('Ctrl Pts',(20.8201275486196,20.6971728954314,14.8879386505139));
#141963=CARTESIAN_POINT('Ctrl Pts',(20.866540268707,20.6272881071107,14.892123284907));
#141964=CARTESIAN_POINT('Ctrl Pts',(20.912886926032,20.5575027911363,14.8963019629909));
#141965=CARTESIAN_POINT('Ctrl Pts',(20.9558733628218,20.4853364119634,14.9004806410749));
#141966=CARTESIAN_POINT('Ctrl Pts',(20.995249084218,20.4111468989766,14.9046593191588));
#141967=CARTESIAN_POINT('Ctrl Pts',(21.0353305871215,20.3356275922885,14.9089128970442));
#141968=CARTESIAN_POINT('Ctrl Pts',(21.0716703524657,20.2580122826047,14.9131664749297));
#141969=CARTESIAN_POINT('Ctrl Pts',(21.1040502914401,20.1787094688203,14.9174200528151));
#141970=CARTESIAN_POINT('Ctrl Pts',(21.1358024821133,20.1009440948279,14.9215911667931));
#141971=CARTESIAN_POINT('Ctrl Pts',(21.1637468322871,20.0215565094717,14.925762280771));
#141972=CARTESIAN_POINT('Ctrl Pts',(21.1877248192282,19.9409551434873,14.929933394749));
#141973=CARTESIAN_POINT('Ctrl Pts',(21.2116947601242,19.8603808240695,14.9341031090693));
#141974=CARTESIAN_POINT('Ctrl Pts',(21.2317008500142,19.7785939734877,14.9382728233897));
#141975=CARTESIAN_POINT('Ctrl Pts',(21.2476340898708,19.6960192390404,14.9424425377101));
#141976=CARTESIAN_POINT('Ctrl Pts',(21.2635667627544,19.6134474429565,14.9466121036541));
#141977=CARTESIAN_POINT('Ctrl Pts',(21.2754267874401,19.5300882706128,14.9507816695982));
#141978=CARTESIAN_POINT('Ctrl Pts',(21.2831563307877,19.4463762970336,14.9549512355422));
#141979=CARTESIAN_POINT('Ctrl Pts',(21.2911576353439,19.3597211137331,14.9592673982812));
#141980=CARTESIAN_POINT('Ctrl Pts',(21.2947325504218,19.2726883838095,14.9635835610201));
#141981=CARTESIAN_POINT('Ctrl Pts',(21.2938756072079,19.1857636052077,14.967899723759));
#141982=CARTESIAN_POINT('Ctrl Pts',(21.293046578829,19.1016703921261,14.9720752879507));
#141983=CARTESIAN_POINT('Ctrl Pts',(21.2880700686645,19.0176786727669,14.9762508521424));
#141984=CARTESIAN_POINT('Ctrl Pts',(21.2789941177452,18.9342240244486,14.980426416334));
#141985=CARTESIAN_POINT('Ctrl Pts',(21.269459762121,18.8465542802383,14.9848128783466));
#141986=CARTESIAN_POINT('Ctrl Pts',(21.2554010498833,18.7594778642489,14.9891993403591));
#141987=CARTESIAN_POINT('Ctrl Pts',(21.2369341836445,18.6734867700757,14.9935858023717));
#141988=CARTESIAN_POINT('Ctrl Pts',(21.2184673174058,18.5874956759025,14.9979722643842));
#141989=CARTESIAN_POINT('Ctrl Pts',(21.1955925215496,18.5025904439985,15.0023587263968));
#141990=CARTESIAN_POINT('Ctrl Pts',(21.1684852750763,18.4192415485537,15.0067451884093));
#141991=CARTESIAN_POINT('Ctrl Pts',(21.1426284959746,18.3397375686859,15.0109293012962));
#141992=CARTESIAN_POINT('Ctrl Pts',(21.1128249191573,18.2613536084881,15.015113414183));
#141993=CARTESIAN_POINT('Ctrl Pts',(21.079190343033,18.1845097394789,15.0192975270699));
#141994=CARTESIAN_POINT('Ctrl Pts',(21.0456010518531,18.1077693315725,15.0234760065479));
#141995=CARTESIAN_POINT('Ctrl Pts',(21.0081911857072,18.0325653152852,15.0276544860259));
#141996=CARTESIAN_POINT('Ctrl Pts',(20.9671260875766,17.9593020024844,15.0318329655039));
#141997=CARTESIAN_POINT('Ctrl Pts',(20.9250013379249,17.8841481893707,15.0361192672527));
#141998=CARTESIAN_POINT('Ctrl Pts',(20.8790302462392,17.8110370933069,15.0404055690016));
#141999=CARTESIAN_POINT('Ctrl Pts',(20.829443678116,17.740382513417,15.0446918707505));
#142000=CARTESIAN_POINT('Ctrl Pts',(20.7811918107953,17.6716297131431,15.0488627999177));
#142001=CARTESIAN_POINT('Ctrl Pts',(20.7295169255159,17.6052032571564,15.0530337290848));
#142002=CARTESIAN_POINT('Ctrl Pts',(20.6746769356327,17.5414572387916,15.0572046582519));
#142003=CARTESIAN_POINT('Ctrl Pts',(20.6175615422498,17.4750662908128,15.0615486462917));
#142004=CARTESIAN_POINT('Ctrl Pts',(20.5570129607975,17.4115834945697,15.0658926343315));
#142005=CARTESIAN_POINT('Ctrl Pts',(20.4933694385991,17.3513712256143,15.0702366223712));
#142006=CARTESIAN_POINT('Ctrl Pts',(20.4297259164008,17.2911589566588,15.074580610411));
#142007=CARTESIAN_POINT('Ctrl Pts',(20.3629878634338,17.2342176031351,15.0789245984507));
#142008=CARTESIAN_POINT('Ctrl Pts',(20.2935357313021,17.1808649545432,15.0832685864905));
#142009=CARTESIAN_POINT('Origin',(18.734,19.211,-1.76670989022852));
#142010=CARTESIAN_POINT('',(20.2935357313021,17.1808649545432,15.9499155261591));
#142011=CARTESIAN_POINT('',(20.2954006413529,17.1784744524704,15.8832287081017));
#142012=CARTESIAN_POINT('',(20.2935357313021,17.1808649545432,-1.76670989022852));
#142013=CARTESIAN_POINT('',(16.174000571626,19.2092892327452,15.4332901097416));
#142014=CARTESIAN_POINT('Ctrl Pts',(16.1740005716256,19.2092892333484,15.4332901097715));
#142015=CARTESIAN_POINT('Ctrl Pts',(16.1739440307447,19.2938972788889,15.437482057942));
#142016=CARTESIAN_POINT('Ctrl Pts',(16.1780862675835,19.3785303101354,15.4416740061124));
#142017=CARTESIAN_POINT('Ctrl Pts',(16.1864081330308,19.4627452667924,15.4458659542829));
#142018=CARTESIAN_POINT('Ctrl Pts',(16.1947304086796,19.5469643745742,15.4500581090829));
#142019=CARTESIAN_POINT('Ctrl Pts',(16.2072326772703,19.6307649161166,15.4542502638829));
#142020=CARTESIAN_POINT('Ctrl Pts',(16.2238439368849,19.713709199047,15.458442418683));
#142021=CARTESIAN_POINT('Ctrl Pts',(16.2404607969944,19.7966814466863,15.4626359868702));
#142022=CARTESIAN_POINT('Ctrl Pts',(16.261189311038,19.8787964183332,15.4668295550574));
#142023=CARTESIAN_POINT('Ctrl Pts',(16.2859076895266,19.9596281048698,15.4710231232447));
#142024=CARTESIAN_POINT('Ctrl Pts',(16.3106584247115,20.0405656011923,15.4752221808702));
#142025=CARTESIAN_POINT('Ctrl Pts',(16.3394093150967,20.1202160261802,15.4794212384956));
#142026=CARTESIAN_POINT('Ctrl Pts',(16.3719892689075,20.1981703531832,15.4836202961211));
#142027=CARTESIAN_POINT('Ctrl Pts',(16.4045936038559,20.2761830171373,15.4878224961023));
#142028=CARTESIAN_POINT('Ctrl Pts',(16.4410325111314,20.3524966484666,15.4920246960834));
#142029=CARTESIAN_POINT('Ctrl Pts',(16.4810885578785,20.426726134439,15.4962268960645));
#142030=CARTESIAN_POINT('Ctrl Pts',(16.5212156880345,20.5010873479616,15.5004365532643));
#142031=CARTESIAN_POINT('Ctrl Pts',(16.5649725361191,20.5733566470847,15.5046462104641));
#142032=CARTESIAN_POINT('Ctrl Pts',(16.6120981192869,20.6431775059769,15.5088558676639));
#142033=CARTESIAN_POINT('Ctrl Pts',(16.6314200308982,20.6718046841136,15.5105818648583));
#142034=CARTESIAN_POINT('Ctrl Pts',(16.6513077816385,20.700020648932,15.5123078620526));
#142035=CARTESIAN_POINT('Ctrl Pts',(16.6717415022698,20.7278025212728,15.5140338592469));
#142036=CARTESIAN_POINT('Ctrl Pts',(16.7212825156696,20.7951589334866,15.5182184936399));
#142037=CARTESIAN_POINT('Ctrl Pts',(16.7742191330187,20.8602110167103,15.522403128033));
#142038=CARTESIAN_POINT('Ctrl Pts',(16.8303093008605,20.9225962497066,15.526587762426));
#142039=CARTESIAN_POINT('Ctrl Pts',(16.8863196312909,20.9848926850454,15.53076644051));
#142040=CARTESIAN_POINT('Ctrl Pts',(16.9454742913218,21.044529470903,15.5349451185939));
#142041=CARTESIAN_POINT('Ctrl Pts',(17.0074891937054,21.1011747103768,15.5391237966779));
#142042=CARTESIAN_POINT('Ctrl Pts',(17.0706156686449,21.1588352750579,15.5433773745633));
#142043=CARTESIAN_POINT('Ctrl Pts',(17.1367056485331,21.2133956031449,15.5476309524487));
#142044=CARTESIAN_POINT('Ctrl Pts',(17.2054179892121,21.2645425577026,15.5518845303342));
#142045=CARTESIAN_POINT('Ctrl Pts',(17.2727982070859,21.314697928741,15.5560556443121));
#142046=CARTESIAN_POINT('Ctrl Pts',(17.3426996279385,21.3615708076596,15.5602267582901));
#142047=CARTESIAN_POINT('Ctrl Pts',(17.4147663076934,21.4049057557432,15.564397872268));
#142048=CARTESIAN_POINT('Ctrl Pts',(17.4868088047781,21.4482261623665,15.5685675865884));
#142049=CARTESIAN_POINT('Ctrl Pts',(17.561014723861,21.4880107590573,15.5727373009088));
#142050=CARTESIAN_POINT('Ctrl Pts',(17.6370000578042,21.5240480165406,15.5769070152292));
#142051=CARTESIAN_POINT('Ctrl Pts',(17.7129826878631,21.5600839916636,15.5810765811732));
#142052=CARTESIAN_POINT('Ctrl Pts',(17.7907441908666,21.5923726963449,15.5852461471172));
#142053=CARTESIAN_POINT('Ctrl Pts',(17.8698781766135,21.6207496704735,15.5894157130613));
#142054=CARTESIAN_POINT('Ctrl Pts',(17.951794415677,21.6501243440057,15.5937318758002));
#142055=CARTESIAN_POINT('Ctrl Pts',(18.0351809497172,21.6753069180702,15.5980480385391));
#142056=CARTESIAN_POINT('Ctrl Pts',(18.119569008403,21.6961709310559,15.602364201278));
#142057=CARTESIAN_POINT('Ctrl Pts',(18.2012081349532,21.7163553010131,15.6065397654697));
#142058=CARTESIAN_POINT('Ctrl Pts',(18.2837840674898,21.7324980994093,15.6107153296614));
#142059=CARTESIAN_POINT('Ctrl Pts',(18.3668630221883,21.7445371399534,15.6148908938531));
#142060=CARTESIAN_POINT('Ctrl Pts',(18.4541380973871,21.7571842438152,15.6192773558656));
#142061=CARTESIAN_POINT('Ctrl Pts',(18.5419677640929,21.7653020795901,15.6236638178781));
#142062=CARTESIAN_POINT('Ctrl Pts',(18.6298465962985,21.7688803858854,15.6280502798907));
#142063=CARTESIAN_POINT('Ctrl Pts',(18.7177254285041,21.7724586921808,15.6324367419032));
#142064=CARTESIAN_POINT('Ctrl Pts',(18.8056528468587,21.771497551399,15.6368232039158));
#142065=CARTESIAN_POINT('Ctrl Pts',(18.8931294701918,21.7660494734381,15.6412096659283));
#142066=CARTESIAN_POINT('Ctrl Pts',(18.9765811644138,21.7608520696202,15.6453943003213));
#142067=CARTESIAN_POINT('Ctrl Pts',(19.0599332586381,21.7515522106696,15.6495789347144));
#142068=CARTESIAN_POINT('Ctrl Pts',(19.1427499109294,21.7381571993675,15.6537635691074));
#142069=CARTESIAN_POINT('Ctrl Pts',(19.225448683967,21.7247812542061,15.6579422471914));
#142070=CARTESIAN_POINT('Ctrl Pts',(19.3076130786653,21.7073218076316,15.6621209252753));
#142071=CARTESIAN_POINT('Ctrl Pts',(19.388810251214,21.6858380825632,15.6662996033593));
#142072=CARTESIAN_POINT('Ctrl Pts',(19.4714628247252,21.6639692771631,15.6705531812447));
#142073=CARTESIAN_POINT('Ctrl Pts',(19.5531126789051,21.6379305338182,15.6748067591302));
#142074=CARTESIAN_POINT('Ctrl Pts',(19.6333118602839,21.6078392056942,15.6790603370156));
#142075=CARTESIAN_POINT('Ctrl Pts',(19.7119562240359,21.5783312566842,15.6832314509935));
#142076=CARTESIAN_POINT('Ctrl Pts',(19.7892052107347,21.5449266242311,15.6874025649715));
#142077=CARTESIAN_POINT('Ctrl Pts',(19.8646513710675,21.5077863368418,15.6915736789494));
#142078=CARTESIAN_POINT('Ctrl Pts',(19.9400722147125,21.4706585122347,15.6957433932698));
#142079=CARTESIAN_POINT('Ctrl Pts',(20.0136910210535,21.4297977252414,15.6999131075902));
#142080=CARTESIAN_POINT('Ctrl Pts',(20.0851220716649,21.3854123683101,15.7040828219106));
#142081=CARTESIAN_POINT('Ctrl Pts',(20.156550580453,21.3410285908003,15.7082523878546));
#142082=CARTESIAN_POINT('Ctrl Pts',(20.2257910980039,21.2931207362392,15.7124219537986));
#142083=CARTESIAN_POINT('Ctrl Pts',(20.2924853680827,21.2419414953347,15.7165915197427));
#142084=CARTESIAN_POINT('Ctrl Pts',(20.3615245264211,21.1889628554564,15.7209076824816));
#142085=CARTESIAN_POINT('Ctrl Pts',(20.4278346353059,21.1324788262494,15.7252238452205));
#142086=CARTESIAN_POINT('Ctrl Pts',(20.4910556240458,21.0728151181063,15.7295400079595));
#142087=CARTESIAN_POINT('Ctrl Pts',(20.5522171957272,21.0150949489804,15.7337155721511));
#142088=CARTESIAN_POINT('Ctrl Pts',(20.6104875206308,20.9543994482413,15.7378911363428));
#142089=CARTESIAN_POINT('Ctrl Pts',(20.6655795109702,20.8910596991774,15.7420667005345));
#142090=CARTESIAN_POINT('Ctrl Pts',(20.7234540667728,20.8245208099644,15.746453162547));
#142091=CARTESIAN_POINT('Ctrl Pts',(20.7778204147506,20.7550639901489,15.7508396245596));
#142092=CARTESIAN_POINT('Ctrl Pts',(20.8283963491848,20.6831086687203,15.7552260865721));
#142093=CARTESIAN_POINT('Ctrl Pts',(20.8789722836189,20.6111533472918,15.7596125485847));
#142094=CARTESIAN_POINT('Ctrl Pts',(20.9257575602053,20.5367000559954,15.7639990105972));
#142095=CARTESIAN_POINT('Ctrl Pts',(20.968526025902,20.4601971179788,15.7683854726097));
#142096=CARTESIAN_POINT('Ctrl Pts',(21.009326651094,20.3872141935449,15.7725701070028));
#142097=CARTESIAN_POINT('Ctrl Pts',(21.0466238491572,20.3120944357929,15.7767547413958));
#142098=CARTESIAN_POINT('Ctrl Pts',(21.0801878476019,20.2352082716739,15.7809393757889));
#142099=CARTESIAN_POINT('Ctrl Pts',(21.1137040718492,20.158431545493,15.7851180538728));
#142100=CARTESIAN_POINT('Ctrl Pts',(21.1434974687764,20.079893825063,15.7892967319568));
#142101=CARTESIAN_POINT('Ctrl Pts',(21.1693835453415,19.9999911197724,15.7934754100407));
#142102=CARTESIAN_POINT('Ctrl Pts',(21.1957336112251,19.9186562159145,15.7977289879261));
#142103=CARTESIAN_POINT('Ctrl Pts',(21.2180346662481,19.8359073320101,15.8019825658116));
#142104=CARTESIAN_POINT('Ctrl Pts',(21.2361429171343,19.7521846470798,15.806236143697));
#142105=CARTESIAN_POINT('Ctrl Pts',(21.2539001042417,19.6700850897683,15.8104072576749));
#142106=CARTESIAN_POINT('Ctrl Pts',(21.2676255061034,19.587049622894,15.8145783716529));
#142107=CARTESIAN_POINT('Ctrl Pts',(21.2772339776254,19.5035080085254,15.8187494856308));
#142108=CARTESIAN_POINT('Ctrl Pts',(21.2868392249321,19.4199944273523,15.8229191999512));
#142109=CARTESIAN_POINT('Ctrl Pts',(21.2923302330118,19.3359754926349,15.8270889142716));
#142110=CARTESIAN_POINT('Ctrl Pts',(21.2936734448665,19.2518883314075,15.8312586285919));
#142111=CARTESIAN_POINT('Ctrl Pts',(21.295016608924,19.1678041623623,15.835428194536));
#142112=CARTESIAN_POINT('Ctrl Pts',(21.2922122637205,19.0836522316219,15.83959776048));
#142113=CARTESIAN_POINT('Ctrl Pts',(21.2852789648471,18.9998705526724,15.8437673264241));
#142114=CARTESIAN_POINT('Ctrl Pts',(21.2781018997384,18.9131432132468,15.848083489163));
#142115=CARTESIAN_POINT('Ctrl Pts',(21.2665001742354,18.8268131717716,15.8523996519019));
#142116=CARTESIAN_POINT('Ctrl Pts',(21.2505527597976,18.7413594915737,15.8567158146408));
#142117=CARTESIAN_POINT('Ctrl Pts',(21.2351248307078,18.6586894560201,15.8608913788325));
#142118=CARTESIAN_POINT('Ctrl Pts',(21.2156301415437,18.5768400108863,15.8650669430242));
#142119=CARTESIAN_POINT('Ctrl Pts',(21.1921916857822,18.4962317606726,15.8692425072158));
#142120=CARTESIAN_POINT('Ctrl Pts',(21.1675694093398,18.4115521793684,15.8736289692284));
#142121=CARTESIAN_POINT('Ctrl Pts',(21.1385946886761,18.3282430251669,15.8780154312409));
#142122=CARTESIAN_POINT('Ctrl Pts',(21.105467444592,18.2467686173742,15.8824018932534));
#142123=CARTESIAN_POINT('Ctrl Pts',(21.0723402005079,18.1652942095816,15.886788355266));
#142124=CARTESIAN_POINT('Ctrl Pts',(21.0350607478797,18.0856550414427,15.8911748172785));
#142125=CARTESIAN_POINT('Ctrl Pts',(20.9938836431738,18.0082839406927,15.8955612792911));
#142126=CARTESIAN_POINT('Ctrl Pts',(20.9545971350278,17.9344652397039,15.8997463422482));
#142127=CARTESIAN_POINT('Ctrl Pts',(20.9116167922617,17.8624361059936,15.9039314052054));
#142128=CARTESIAN_POINT('Ctrl Pts',(20.8651297737837,17.7925903668923,15.9081164681625));
#142129=CARTESIAN_POINT('Ctrl Pts',(20.8187208419221,17.722861951242,15.9122945012559));
#142130=CARTESIAN_POINT('Ctrl Pts',(20.7688171985839,17.6553100179064,15.9164725343493));
#142131=CARTESIAN_POINT('Ctrl Pts',(20.7156518556546,17.5903038770391,15.9206505674427));
#142132=CARTESIAN_POINT('Ctrl Pts',(20.6625380463695,17.5253607472076,15.9248245507312));
#142133=CARTESIAN_POINT('Ctrl Pts',(20.6061691036096,17.4629588649992,15.9289985340196));
#142134=CARTESIAN_POINT('Ctrl Pts',(20.5468208180928,17.4034379176666,15.933172517308));
#142135=CARTESIAN_POINT('Ctrl Pts',(20.4875162743701,17.343960839386,15.9373434242225));
#142136=CARTESIAN_POINT('Ctrl Pts',(20.4252370755919,17.2873608011117,15.941514331137));
#142137=CARTESIAN_POINT('Ctrl Pts',(20.3602977400031,17.2339426763847,15.9456852380515));
#142138=CARTESIAN_POINT('Ctrl Pts',(20.3383431144115,17.2158831302321,15.9470953340874));
#142139=CARTESIAN_POINT('Ctrl Pts',(20.3160847536487,17.1981869578917,15.9485054301233));
#142140=CARTESIAN_POINT('Ctrl Pts',(20.2935357313021,17.1808649545432,15.9499155261591));
#142141=CARTESIAN_POINT('Ctrl Pts',(20.2935357313021,17.1808649545431,15.149955387129));
#142142=CARTESIAN_POINT('Ctrl Pts',(20.2270593312522,17.1297982427999,15.1541321186299));
#142143=CARTESIAN_POINT('Ctrl Pts',(20.157982890463,17.0819316190979,15.1583088501308));
#142144=CARTESIAN_POINT('Ctrl Pts',(20.0866487390076,17.0375370054079,15.1624855816317));
#142145=CARTESIAN_POINT('Ctrl Pts',(20.0153845446641,16.9931859293349,15.166658217029));
#142146=CARTESIAN_POINT('Ctrl Pts',(19.9418674289854,16.9523003382024,15.1708308524263));
#142147=CARTESIAN_POINT('Ctrl Pts',(19.866470098234,16.915109872706,15.1750034878237));
#142148=CARTESIAN_POINT('Ctrl Pts',(19.7911122885109,16.8779389013406,15.1791739360502));
#142149=CARTESIAN_POINT('Ctrl Pts',(19.713876632298,16.8444594130657,15.1833443842767));
#142150=CARTESIAN_POINT('Ctrl Pts',(19.6351609058952,16.8148553838121,15.1875148325032));
#142151=CARTESIAN_POINT('Ctrl Pts',(19.5564628268888,16.7852579915301,15.1916843457507));
#142152=CARTESIAN_POINT('Ctrl Pts',(19.476285767298,16.7595344941138,15.1958538589982));
#142153=CARTESIAN_POINT('Ctrl Pts',(19.39504670236,16.7378204154775,15.2000233722457));
#142154=CARTESIAN_POINT('Ctrl Pts',(19.3138014809693,16.7161046913065,15.2041932014669));
#142155=CARTESIAN_POINT('Ctrl Pts',(19.2314945392017,16.6983991067548,15.2083630306881));
#142156=CARTESIAN_POINT('Ctrl Pts',(19.1485558711826,16.6847887203031,15.2125328599093));
#142157=CARTESIAN_POINT('Ctrl Pts',(19.0655304067008,16.6711640903938,15.2167070529145));
#142158=CARTESIAN_POINT('Ctrl Pts',(18.9818723507359,16.6616432910686,15.2208812459196));
#142159=CARTESIAN_POINT('Ctrl Pts',(18.8980192099718,16.6562597590439,15.2250554389248));
#142160=CARTESIAN_POINT('Ctrl Pts',(18.8141207284214,16.6508733160541,15.2292318889854));
#142161=CARTESIAN_POINT('Ctrl Pts',(18.7300274122327,16.6496286018667,15.2334083390461));
#142162=CARTESIAN_POINT('Ctrl Pts',(18.6461767343805,16.6525068743466,15.2375847891067));
#142163=CARTESIAN_POINT('Ctrl Pts',(18.5621801887309,16.6553901539089,15.2417685045776));
#142164=CARTESIAN_POINT('Ctrl Pts',(18.4784275833816,16.6624107077525,15.2459522200485));
#142165=CARTESIAN_POINT('Ctrl Pts',(18.3953510240905,16.6734979071702,15.2501359355193));
#142166=CARTESIAN_POINT('Ctrl Pts',(18.3321635993764,16.6819307501343,15.2533180389742));
#142167=CARTESIAN_POINT('Ctrl Pts',(18.2693671588674,16.6927150749222,15.2565001424291));
#142168=CARTESIAN_POINT('Ctrl Pts',(18.2071464487601,16.7058003401833,15.259682245884));
#142169=CARTESIAN_POINT('Ctrl Pts',(18.125322923169,16.7230081562804,15.2638668802771));
#142170=CARTESIAN_POINT('Ctrl Pts',(18.0441910630359,16.74426092691,15.2680515146701));
#142171=CARTESIAN_POINT('Ctrl Pts',(17.9641810754836,16.7694884142285,15.2722361490632));
#142172=CARTESIAN_POINT('Ctrl Pts',(17.8842849722453,16.7946799933414,15.2764148271471));
#142173=CARTESIAN_POINT('Ctrl Pts',(17.8055080047355,16.8238349143801,15.2805935052311));
#142174=CARTESIAN_POINT('Ctrl Pts',(17.7282699071042,16.8568319982967,15.284772183315));
#142175=CARTESIAN_POINT('Ctrl Pts',(17.6496473720828,16.8904205312279,15.2890257612004));
#142176=CARTESIAN_POINT('Ctrl Pts',(17.5726198898781,16.92799022417,15.2932793390859));
#142177=CARTESIAN_POINT('Ctrl Pts',(17.4976137413829,16.969360194076,15.2975329169713));
#142178=CARTESIAN_POINT('Ctrl Pts',(17.4240617334388,17.0099281263886,15.3017040309493));
#142179=CARTESIAN_POINT('Ctrl Pts',(17.3524538049873,17.0541500666244,15.3058751449272));
#142180=CARTESIAN_POINT('Ctrl Pts',(17.2831698439506,17.1018077711367,15.3100462589052));
#142181=CARTESIAN_POINT('Ctrl Pts',(17.213909131816,17.1494494836459,15.3142159732255));
#142182=CARTESIAN_POINT('Ctrl Pts',(17.1469712170492,17.2005244102484,15.3183856875459));
#142183=CARTESIAN_POINT('Ctrl Pts',(17.0827076373572,17.2547705827083,15.3225554018663));
#142184=CARTESIAN_POINT('Ctrl Pts',(17.0184463444392,17.3090148248565,15.3267249678103));
#142185=CARTESIAN_POINT('Ctrl Pts',(16.9568595483703,17.3664297911051,15.3308945337544));
#142186=CARTESIAN_POINT('Ctrl Pts',(16.8982652087742,17.4267136507043,15.3350640996984));
#142187=CARTESIAN_POINT('Ctrl Pts',(16.8376107644817,17.4891170164388,15.3393802624373));
#142188=CARTESIAN_POINT('Ctrl Pts',(16.7801634890497,17.5545943914717,15.3436964251763));
#142189=CARTESIAN_POINT('Ctrl Pts',(16.7262325806843,17.6227714301982,15.3480125879152));
#142190=CARTESIAN_POINT('Ctrl Pts',(16.6740584659865,17.6887276090592,15.3521881521069));
#142191=CARTESIAN_POINT('Ctrl Pts',(16.6251753803871,17.7572098587054,15.3563637162985));
#142192=CARTESIAN_POINT('Ctrl Pts',(16.5798195291699,17.8278490685777,15.3605392804902));
#142193=CARTESIAN_POINT('Ctrl Pts',(16.5321728617311,17.9020560970119,15.3649257425027));
#142194=CARTESIAN_POINT('Ctrl Pts',(16.4884194038191,17.9786432012271,15.3693122045153));
#142195=CARTESIAN_POINT('Ctrl Pts',(16.4487777573747,18.0571545589593,15.3736986665278));
#142196=CARTESIAN_POINT('Ctrl Pts',(16.4091361109302,18.1356659166915,15.3780851285404));
#142197=CARTESIAN_POINT('Ctrl Pts',(16.3736064408138,18.2161009664617,15.3824715905529));
#142198=CARTESIAN_POINT('Ctrl Pts',(16.3423477078172,18.2979833992217,15.3868580525655));
#142199=CARTESIAN_POINT('Ctrl Pts',(16.3083133302776,18.3871366489943,15.3916340140293));
#142200=CARTESIAN_POINT('Ctrl Pts',(16.2792349760219,18.4782809296076,15.396409975493));
#142201=CARTESIAN_POINT('Ctrl Pts',(16.2553188691388,18.5708907503302,15.4011859369568));
#142202=CARTESIAN_POINT('Ctrl Pts',(16.2315006236311,18.6631216245767,15.4059423558521));
#142203=CARTESIAN_POINT('Ctrl Pts',(16.2128025911618,18.756805887815,15.4106987747473));
#142204=CARTESIAN_POINT('Ctrl Pts',(16.1993817363335,18.8514026453261,15.4154551936426));
#142205=CARTESIAN_POINT('Ctrl Pts',(16.1860549755608,18.9453361818529,15.4201782651283));
#142206=CARTESIAN_POINT('Ctrl Pts',(16.1779317634136,19.0401692636772,15.4249013366139));
#142207=CARTESIAN_POINT('Ctrl Pts',(16.1751178968034,19.1353535728534,15.4296244080995));
#142208=CARTESIAN_POINT('Ctrl Pts',(16.1743899245164,19.1599785991389,15.4308463086469));
#142209=CARTESIAN_POINT('Ctrl Pts',(16.1740170525925,19.1846270439603,15.4320682091943));
#142210=CARTESIAN_POINT('Ctrl Pts',(16.174000571626,19.2092892327452,15.4332901097416));
#142211=CARTESIAN_POINT('',(16.1740008768645,19.213118854712,15.3667098902285));
#142212=CARTESIAN_POINT('Ctrl Pts',(20.2935357313021,17.1808649545432,15.0832685864905));
#142213=CARTESIAN_POINT('Ctrl Pts',(20.2260494003338,17.1290224208383,15.0874896205405));
#142214=CARTESIAN_POINT('Ctrl Pts',(20.15600103177,17.0805683880659,15.0917106545905));
#142215=CARTESIAN_POINT('Ctrl Pts',(20.0837719748573,17.0357492981521,15.0959316886405));
#142216=CARTESIAN_POINT('Ctrl Pts',(20.0123180844573,16.9914112093633,15.1001074223034));
#142217=CARTESIAN_POINT('Ctrl Pts',(19.9387305254191,16.9506305872145,15.1042831559662));
#142218=CARTESIAN_POINT('Ctrl Pts',(19.8634030708264,16.9135995769984,15.108458889629));
#142219=CARTESIAN_POINT('Ctrl Pts',(19.7868498330056,16.8759659712017,15.1127025738726));
#142220=CARTESIAN_POINT('Ctrl Pts',(19.7085000246848,16.8422052935393,15.1169462581162));
#142221=CARTESIAN_POINT('Ctrl Pts',(19.6287860049645,16.8124675309015,15.1211899423598));
#142222=CARTESIAN_POINT('Ctrl Pts',(19.5490719852442,16.7827297682637,15.1254336266034));
#142223=CARTESIAN_POINT('Ctrl Pts',(19.467994242552,16.7570150062661,15.1296773108471));
#142224=CARTESIAN_POINT('Ctrl Pts',(19.3859971465604,16.7354193164275,15.1339209950907));
#142225=CARTESIAN_POINT('Ctrl Pts',(19.3051410205342,16.7141241254443,15.1381056294837));
#142226=CARTESIAN_POINT('Ctrl Pts',(19.2230900288855,16.6967547916185,15.1422902638768));
#142227=CARTESIAN_POINT('Ctrl Pts',(19.140260221412,16.6834413691275,15.1464748982698));
#142228=CARTESIAN_POINT('Ctrl Pts',(19.0575483119171,16.6701468966454,15.1506535763538));
#142229=CARTESIAN_POINT('Ctrl Pts',(18.9740602388407,16.66089694071,15.1548322544377));
#142230=CARTESIAN_POINT('Ctrl Pts',(18.8902255245013,16.6557713242267,15.1590109325216));
#142231=CARTESIAN_POINT('Ctrl Pts',(18.8048881331583,16.6505538347516,15.1632645104071));
#142232=CARTESIAN_POINT('Ctrl Pts',(18.7191920174707,16.6496101194126,15.1675180882925));
#142233=CARTESIAN_POINT('Ctrl Pts',(18.6335993142648,16.652969565798,15.171771666178));
#142234=CARTESIAN_POINT('Ctrl Pts',(18.549665992631,16.6562638827597,15.1759427801559));
#142235=CARTESIAN_POINT('Ctrl Pts',(18.4658325904041,16.6636959811426,15.1801138941339));
#142236=CARTESIAN_POINT('Ctrl Pts',(18.3825365202428,16.6752410559367,15.1842850081118));
#142237=CARTESIAN_POINT('Ctrl Pts',(18.2992684008824,16.6867822566694,15.1884547224322));
#142238=CARTESIAN_POINT('Ctrl Pts',(18.2165377107927,16.70243362971,15.1926244367525));
#142239=CARTESIAN_POINT('Ctrl Pts',(18.1347761196918,16.7221185762941,15.1967941510729));
#142240=CARTESIAN_POINT('Ctrl Pts',(18.0530174380192,16.7418028224032,15.200963717017));
#142241=CARTESIAN_POINT('Ctrl Pts',(17.9722282338244,16.7655202481684,15.205133282961));
#142242=CARTESIAN_POINT('Ctrl Pts',(17.8928280294743,16.7931435700187,15.209302848905));
#142243=CARTESIAN_POINT('Ctrl Pts',(17.8106362118899,16.8217380937883,15.213619011644));
#142244=CARTESIAN_POINT('Ctrl Pts',(17.7299333840843,16.8545181133117,15.2179351743829));
#142245=CARTESIAN_POINT('Ctrl Pts',(17.6511637413086,16.891287596088,15.2222513371218));
#142246=CARTESIAN_POINT('Ctrl Pts',(17.5749600113613,16.9268593168303,15.2264269013135));
#142247=CARTESIAN_POINT('Ctrl Pts',(17.5005658480124,16.966164316944,15.2306024655052));
#142248=CARTESIAN_POINT('Ctrl Pts',(17.4283578509306,17.0089785244977,15.2347780296969));
#142249=CARTESIAN_POINT('Ctrl Pts',(17.3525027995743,17.0539551758939,15.2391644917094));
#142250=CARTESIAN_POINT('Ctrl Pts',(17.2790610511154,17.1028045279329,15.243550953722));
#142251=CARTESIAN_POINT('Ctrl Pts',(17.2084323379752,17.1552171056787,15.2479374157345));
#142252=CARTESIAN_POINT('Ctrl Pts',(17.137803624835,17.2076296834245,15.252323877747));
#142253=CARTESIAN_POINT('Ctrl Pts',(17.0699883460668,17.2636050588652,15.2567103397596));
#142254=CARTESIAN_POINT('Ctrl Pts',(17.0053421035811,17.3227887096121,15.2610968017721));
#142255=CARTESIAN_POINT('Ctrl Pts',(16.9445899812052,17.3784072924496,15.2652190348167));
#142256=CARTESIAN_POINT('Ctrl Pts',(16.8863955977243,17.4370795204071,15.2693412678613));
#142257=CARTESIAN_POINT('Ctrl Pts',(16.8310887538612,17.4985372152019,15.2734635009059));
#142258=CARTESIAN_POINT('Ctrl Pts',(16.7758743514516,17.5598921878336,15.2775788439313));
#142259=CARTESIAN_POINT('Ctrl Pts',(16.7235382140142,17.6240230272318,15.2816941869568));
#142260=CARTESIAN_POINT('Ctrl Pts',(16.6743754759291,17.6906228034315,15.2858095299822));
#142261=CARTESIAN_POINT('Ctrl Pts',(16.6252589923635,17.7571599195604,15.2899210011074));
#142262=CARTESIAN_POINT('Ctrl Pts',(16.5793102664133,17.8261609852053,15.2940324722327));
#142263=CARTESIAN_POINT('Ctrl Pts',(16.5367853878605,17.8972846776411,15.2981439433579));
#142264=CARTESIAN_POINT('Ctrl Pts',(16.4942868717928,17.9683642783041,15.3022528656553));
#142265=CARTESIAN_POINT('Ctrl Pts',(16.4552082342176,18.0415634879277,15.3063617879526));
#142266=CARTESIAN_POINT('Ctrl Pts',(16.4197623875935,18.1165118669794,15.31047071025));
#142267=CARTESIAN_POINT('Ctrl Pts',(16.3843271437776,18.1914378269504,15.3145784034579));
#142268=CARTESIAN_POINT('Ctrl Pts',(16.3525227351488,18.2681114878987,15.3186860966658));
#142269=CARTESIAN_POINT('Ctrl Pts',(16.3245154961046,18.3461390715913,15.3227937898737));
#142270=CARTESIAN_POINT('Ctrl Pts',(16.2964946934756,18.4242044431483,15.3269034723904));
#142271=CARTESIAN_POINT('Ctrl Pts',(16.2722748983311,18.5036246009546,15.331013154907));
#142272=CARTESIAN_POINT('Ctrl Pts',(16.2519734104525,18.5839880313907,15.3351228374237));
#142273=CARTESIAN_POINT('Ctrl Pts',(16.2316667383952,18.664371983396,15.339233569387));
#142274=CARTESIAN_POINT('Ctrl Pts',(16.2152804642371,18.7456992225571,15.3433443013503));
#142275=CARTESIAN_POINT('Ctrl Pts',(16.2028808242116,18.8275476327413,15.3474550333136));
#142276=CARTESIAN_POINT('Ctrl Pts',(16.1904661338127,18.9094953884816,15.3515707547807));
#142277=CARTESIAN_POINT('Ctrl Pts',(16.1820477886727,18.9919651056506,15.3556864762478));
#142278=CARTESIAN_POINT('Ctrl Pts',(16.1776401048969,19.0745299054429,15.3598021977149));
#142279=CARTESIAN_POINT('Ctrl Pts',(16.175174200724,19.1207212600628,15.3621047618861));
#142280=CARTESIAN_POINT('Ctrl Pts',(16.173962657598,19.1669423575626,15.3644073260573));
#142281=CARTESIAN_POINT('Ctrl Pts',(16.1740008768645,19.213118854712,15.3667098902285));
#142282=CARTESIAN_POINT('Ctrl Pts',(16.1723624648697,19.2131202107894,15.3667098902285));
#142283=CARTESIAN_POINT('Ctrl Pts',(16.1710770500739,19.3573559412274,15.3738974629702));
#142284=CARTESIAN_POINT('Ctrl Pts',(16.2478506686825,20.350918062683,15.4234769712723));
#142285=CARTESIAN_POINT('Ctrl Pts',(17.5479306856132,21.9960550376254,15.515448415135));
#142286=CARTESIAN_POINT('Ctrl Pts',(20.4337937178339,21.715794062981,15.6426242218164));
#142287=CARTESIAN_POINT('Ctrl Pts',(21.7124086289,19.2304391852282,15.7652176528054));
#142288=CARTESIAN_POINT('Ctrl Pts',(20.8926534908113,17.6447068409585,15.8454191482338));
#142289=CARTESIAN_POINT('Ctrl Pts',(20.2954006413529,17.1784744524704,15.8832287081017));
#142290=CARTESIAN_POINT('Origin',(18.734,19.211,-1.76670989022852));
#142291=CARTESIAN_POINT('',(20.2935357313021,17.1808649545432,16.7498176665395));
#142292=CARTESIAN_POINT('',(20.2935357313021,17.1808649545431,16.6833822583817));
#142293=CARTESIAN_POINT('',(20.2935357313021,17.1808649545432,-1.76670989022852));
#142294=CARTESIAN_POINT('',(16.1740007055014,19.2129005700936,16.2332901098004));
#142295=CARTESIAN_POINT('Ctrl Pts',(16.1740007055014,19.2129005700936,16.2332901098004));
#142296=CARTESIAN_POINT('Ctrl Pts',(16.1740727513108,19.3099436741144,16.2381006886061));
#142297=CARTESIAN_POINT('Ctrl Pts',(16.1796667621362,19.4067618611662,16.2429112674118));
#142298=CARTESIAN_POINT('Ctrl Pts',(16.1906824963736,19.5027808693996,16.2477218462175));
#142299=CARTESIAN_POINT('Ctrl Pts',(16.201890345519,19.6004744535201,16.2526163217372));
#142300=CARTESIAN_POINT('Ctrl Pts',(16.218710639996,19.6973405506009,16.2575107972568));
#142301=CARTESIAN_POINT('Ctrl Pts',(16.2409867483461,19.7927945746377,16.2624052727765));
#142302=CARTESIAN_POINT('Ctrl Pts',(16.2632628566961,19.8882485986746,16.2672997482961));
#142303=CARTESIAN_POINT('Ctrl Pts',(16.2909946214077,19.9822904288897,16.2721942238158));
#142304=CARTESIAN_POINT('Ctrl Pts',(16.3239764935689,20.074357804418,16.2770886993355));
#142305=CARTESIAN_POINT('Ctrl Pts',(16.3521750361989,20.1530727360925,16.2812733337285));
#142306=CARTESIAN_POINT('Ctrl Pts',(16.3842865295797,20.2305511910394,16.2854579681216));
#142307=CARTESIAN_POINT('Ctrl Pts',(16.4201827606335,20.3063765484118,16.2896426025146));
#142308=CARTESIAN_POINT('Ctrl Pts',(16.4560278978456,20.3820939777733,16.2938212805986));
#142309=CARTESIAN_POINT('Ctrl Pts',(16.4956468770878,20.4561625710813,16.2979999586825));
#142310=CARTESIAN_POINT('Ctrl Pts',(16.5388624466769,20.5281830252439,16.3021786367664));
#142311=CARTESIAN_POINT('Ctrl Pts',(16.5828526242924,20.6014943942872,16.3064322146519));
#142312=CARTESIAN_POINT('Ctrl Pts',(16.6305694356436,20.6726830222909,16.3106857925373));
#142313=CARTESIAN_POINT('Ctrl Pts',(16.6817755898824,20.7413512572339,16.3149393704228));
#142314=CARTESIAN_POINT('Ctrl Pts',(16.7319890129006,20.8086882244474,16.3191104844007));
#142315=CARTESIAN_POINT('Ctrl Pts',(16.7855574030483,20.8736012662212,16.3232815983787));
#142316=CARTESIAN_POINT('Ctrl Pts',(16.8422127801055,20.9357437823178,16.3274527123566));
#142317=CARTESIAN_POINT('Ctrl Pts',(16.8988491459038,20.997865445893,16.331622426677));
#142318=CARTESIAN_POINT('Ctrl Pts',(16.9585701316818,21.0572180904717,16.3357921409973));
#142319=CARTESIAN_POINT('Ctrl Pts',(17.0210683042879,21.1134891605013,16.3399618553177));
#142320=CARTESIAN_POINT('Ctrl Pts',(17.0835642529408,21.1697582281647,16.3441314212618));
#142321=CARTESIAN_POINT('Ctrl Pts',(17.1488368494857,21.2229456321214,16.3483009872058));
#142322=CARTESIAN_POINT('Ctrl Pts',(17.2165437463578,21.2727775142537,16.3524705531499));
#142323=CARTESIAN_POINT('Ctrl Pts',(17.2866311341984,21.3243614238875,16.3567867158888));
#142324=CARTESIAN_POINT('Ctrl Pts',(17.3593267625536,21.3723491485032,16.3611028786277));
#142325=CARTESIAN_POINT('Ctrl Pts',(17.4342176396321,21.4164853923063,16.3654190413666));
#142326=CARTESIAN_POINT('Ctrl Pts',(17.5066689542669,21.4591839026099,16.3695946055583));
#142327=CARTESIAN_POINT('Ctrl Pts',(17.5811742544608,21.4982778256331,16.37377016975));
#142328=CARTESIAN_POINT('Ctrl Pts',(17.6573356824291,21.533583464005,16.3779457339417));
#142329=CARTESIAN_POINT('Ctrl Pts',(17.7373438430675,21.5706723062399,16.3823321959542));
#142330=CARTESIAN_POINT('Ctrl Pts',(17.8191792885613,21.6035798961265,16.3867186579667));
#142331=CARTESIAN_POINT('Ctrl Pts',(17.9023606575271,21.6321517928563,16.3911051199793));
#142332=CARTESIAN_POINT('Ctrl Pts',(17.985542026493,21.6607236895861,16.3954915819918));
#142333=CARTESIAN_POINT('Ctrl Pts',(18.0700687402226,21.6849598063577,16.3998780440044));
#142334=CARTESIAN_POINT('Ctrl Pts',(18.1554472698608,21.7047675790756,16.4042645060169));
#142335=CARTESIAN_POINT('Ctrl Pts',(18.2368974067891,21.7236639668085,16.4084491404099));
#142336=CARTESIAN_POINT('Ctrl Pts',(18.3194258684925,21.7386009007969,16.412633774803));
#142337=CARTESIAN_POINT('Ctrl Pts',(18.4026129434633,21.7494606789864,16.416818409196));
#142338=CARTESIAN_POINT('Ctrl Pts',(18.4856816119294,21.7603049996258,16.42099708728));
#142339=CARTESIAN_POINT('Ctrl Pts',(18.5694065793227,21.7670836326581,16.4251757653639));
#142340=CARTESIAN_POINT('Ctrl Pts',(18.65335615196,21.769729483508,16.4293544434479));
#142341=CARTESIAN_POINT('Ctrl Pts',(18.7388104603533,21.772422759333,16.4336080213333));
#142342=CARTESIAN_POINT('Ctrl Pts',(18.8244970356233,21.770833526475,16.4378615992187));
#142343=CARTESIAN_POINT('Ctrl Pts',(18.9099530743145,21.7649460674884,16.4421151771042));
#142344=CARTESIAN_POINT('Ctrl Pts',(18.9937523809418,21.7591727483826,16.4462862910821));
#142345=CARTESIAN_POINT('Ctrl Pts',(19.077329529944,21.7492664079889,16.4504574050601));
#142346=CARTESIAN_POINT('Ctrl Pts',(19.1602480327617,21.7352647671286,16.454628519038));
#142347=CARTESIAN_POINT('Ctrl Pts',(19.243138711475,21.7212678246541,16.4587982333584));
#142348=CARTESIAN_POINT('Ctrl Pts',(19.3253707297096,21.7031783874643,16.4629679476788));
#142349=CARTESIAN_POINT('Ctrl Pts',(19.4065148699746,21.6810857777946,16.4671376619991));
#142350=CARTESIAN_POINT('Ctrl Pts',(19.4876561227829,21.6589939542747,16.4713072279432));
#142351=CARTESIAN_POINT('Ctrl Pts',(19.5677091309384,21.6328993631757,16.4754767938872));
#142352=CARTESIAN_POINT('Ctrl Pts',(19.6462583168593,21.6029416304168,16.4796463598313));
#142353=CARTESIAN_POINT('Ctrl Pts',(19.7275691952563,21.571930620731,16.4839625225702));
#142354=CARTESIAN_POINT('Ctrl Pts',(19.8072680422831,21.5367799467921,16.4882786853091));
#142355=CARTESIAN_POINT('Ctrl Pts',(19.8849166499543,21.4976986825679,16.492594848048));
#142356=CARTESIAN_POINT('Ctrl Pts',(19.9600358623978,21.4598904864152,16.4967704122397));
#142357=CARTESIAN_POINT('Ctrl Pts',(20.0332359708031,21.4184041187291,16.5009459764314));
#142358=CARTESIAN_POINT('Ctrl Pts',(20.104147161879,21.3734746830414,16.5051215406231));
#142359=CARTESIAN_POINT('Ctrl Pts',(20.1786399086407,21.3262759683667,16.5095080026356));
#142360=CARTESIAN_POINT('Ctrl Pts',(20.2506059585102,21.2752775637102,16.5138944646481));
#142361=CARTESIAN_POINT('Ctrl Pts',(20.3196548994211,21.2208006219379,16.5182809266607));
#142362=CARTESIAN_POINT('Ctrl Pts',(20.388703840332,21.1663236801656,16.5226673886732));
#142363=CARTESIAN_POINT('Ctrl Pts',(20.4548352860543,21.1083686408955,16.5270538506858));
#142364=CARTESIAN_POINT('Ctrl Pts',(20.5177042670233,21.0473003806031,16.5314403126983));
#142365=CARTESIAN_POINT('Ctrl Pts',(20.5776805529837,20.9890419614915,16.5356249470914));
#142366=CARTESIAN_POINT('Ctrl Pts',(20.6349112416909,20.9277336646777,16.5398095814844));
#142367=CARTESIAN_POINT('Ctrl Pts',(20.6890701824651,20.8636646912292,16.5439942158775));
#142368=CARTESIAN_POINT('Ctrl Pts',(20.7431520346907,20.7996869120343,16.5481728939614));
#142369=CARTESIAN_POINT('Ctrl Pts',(20.7941705292094,20.7329566097132,16.5523515720454));
#142370=CARTESIAN_POINT('Ctrl Pts',(20.8418355824983,20.6638004533156,16.5565302501293));
#142371=CARTESIAN_POINT('Ctrl Pts',(20.890354997611,20.5934047225164,16.5607838280148));
#142372=CARTESIAN_POINT('Ctrl Pts',(20.9353992222983,20.520495651305,16.5650374059002));
#142373=CARTESIAN_POINT('Ctrl Pts',(20.9767045339426,20.4454538765921,16.5692909837856));
#142374=CARTESIAN_POINT('Ctrl Pts',(21.0172090615201,20.3718669331139,16.5734620977636));
#142375=CARTESIAN_POINT('Ctrl Pts',(21.0541181225502,20.2962296630071,16.5776332117415));
#142376=CARTESIAN_POINT('Ctrl Pts',(21.0872271712958,20.2189295016394,16.5818043257195));
#142377=CARTESIAN_POINT('Ctrl Pts',(21.1203251099804,20.1416552790873,16.5859740400399));
#142378=CARTESIAN_POINT('Ctrl Pts',(21.1496253878361,20.0627196959935,16.5901437543602));
#142379=CARTESIAN_POINT('Ctrl Pts',(21.1749707834402,19.9825320047744,16.5943134686806));
#142380=CARTESIAN_POINT('Ctrl Pts',(21.2003152771465,19.9023471669775,16.5984830346247));
#142381=CARTESIAN_POINT('Ctrl Pts',(21.2217050305799,19.820910748543,16.6026526005687));
#142382=CARTESIAN_POINT('Ctrl Pts',(21.2390325027795,19.7386477613126,16.6068221665128));
#142383=CARTESIAN_POINT('Ctrl Pts',(21.2569691875259,19.6534925089337,16.6111383292517));
#142384=CARTESIAN_POINT('Ctrl Pts',(21.2705525077455,19.5674519980823,16.6154544919906));
#142385=CARTESIAN_POINT('Ctrl Pts',(21.2797210678871,19.4810078600997,16.6197706547295));
#142386=CARTESIAN_POINT('Ctrl Pts',(21.2885909631466,19.3973796308195,16.6239462189212));
#142387=CARTESIAN_POINT('Ctrl Pts',(21.2933293236125,19.3133741398416,16.6281217831129));
#142388=CARTESIAN_POINT('Ctrl Pts',(21.2939336612287,19.2294295987024,16.6322973473046));
#142389=CARTESIAN_POINT('Ctrl Pts',(21.2945685225012,19.1412452183496,16.6366838093171));
#142390=CARTESIAN_POINT('Ctrl Pts',(21.2906407927078,19.0531286901045,16.6410702713296));
#142391=CARTESIAN_POINT('Ctrl Pts',(21.2822091879386,18.965582122686,16.6454567333422));
#142392=CARTESIAN_POINT('Ctrl Pts',(21.2737775831694,18.8780355552674,16.6498431953547));
#142393=CARTESIAN_POINT('Ctrl Pts',(21.2608422640145,18.7910595113906,16.6542296573673));
#142394=CARTESIAN_POINT('Ctrl Pts',(21.2435233083642,18.7051415565825,16.6586161193798));
#142395=CARTESIAN_POINT('Ctrl Pts',(21.2270051786283,18.6231964351316,16.6627997520461));
#142396=CARTESIAN_POINT('Ctrl Pts',(21.2064383857994,18.5419087704169,16.6669833847124));
#142397=CARTESIAN_POINT('Ctrl Pts',(21.1818895089893,18.4617090339659,16.6711670173787));
#142398=CARTESIAN_POINT('Ctrl Pts',(21.1573729381811,18.381614839323,16.6753451444389));
#142399=CARTESIAN_POINT('Ctrl Pts',(21.1288848202261,18.3026061663239,16.6795232714992));
#142400=CARTESIAN_POINT('Ctrl Pts',(21.0965427533354,18.2251035862412,16.6837013985594));
#142401=CARTESIAN_POINT('Ctrl Pts',(21.0642335424463,18.1476797403009,16.6878752810997));
#142402=CARTESIAN_POINT('Ctrl Pts',(21.0280783340578,18.0717593708865,16.6920491636399));
#142403=CARTESIAN_POINT('Ctrl Pts',(20.9882441729213,17.9977468488191,16.6962230461801));
#142404=CARTESIAN_POINT('Ctrl Pts',(20.9484385271439,17.9237873087547,16.7003939408387));
#142405=CARTESIAN_POINT('Ctrl Pts',(20.9049593786091,17.8517333063674,16.7045648354973));
#142406=CARTESIAN_POINT('Ctrl Pts',(20.8580208517661,17.7819669628512,16.7087357301559));
#142407=CARTESIAN_POINT('Ctrl Pts',(20.8110938747848,17.7122177862909,16.7129055985092));
#142408=CARTESIAN_POINT('Ctrl Pts',(20.7607094614797,17.6447555353991,16.7170754668625));
#142409=CARTESIAN_POINT('Ctrl Pts',(20.7071258294302,17.5799345625527,16.7212453352158));
#142410=CARTESIAN_POINT('Ctrl Pts',(20.6535492745797,17.5151221511065,16.7254146528228));
#142411=CARTESIAN_POINT('Ctrl Pts',(20.596774638735,17.4529506748439,16.7295839704299));
#142412=CARTESIAN_POINT('Ctrl Pts',(20.537100285066,17.3937412506759,16.7337532880369));
#142413=CARTESIAN_POINT('Ctrl Pts',(20.4773989743761,17.3345050795122,16.7379244890724));
#142414=CARTESIAN_POINT('Ctrl Pts',(20.4147956627377,17.2782339503688,16.742095690108));
#142415=CARTESIAN_POINT('Ctrl Pts',(20.3496246776528,17.2252112647718,16.7462668911436));
#142416=CARTESIAN_POINT('Ctrl Pts',(20.3311321996355,17.2101659060658,16.7474504829422));
#142417=CARTESIAN_POINT('Ctrl Pts',(20.3124331846543,17.1953818477909,16.7486340747409));
#142418=CARTESIAN_POINT('Ctrl Pts',(20.2935357313021,17.1808649545432,16.7498176665395));
#142419=CARTESIAN_POINT('Ctrl Pts',(20.2935357313021,17.1808649545432,15.9499155261591));
#142420=CARTESIAN_POINT('Ctrl Pts',(20.226860236598,17.1296452996606,15.9540850572956));
#142421=CARTESIAN_POINT('Ctrl Pts',(20.1576411597185,17.0817002678535,15.9582545884321));
#142422=CARTESIAN_POINT('Ctrl Pts',(20.0862377111805,17.0372812572779,15.9624241195686));
#142423=CARTESIAN_POINT('Ctrl Pts',(20.0148299716009,16.9928595773099,15.966593901276));
#142424=CARTESIAN_POINT('Ctrl Pts',(19.9412379910235,16.9519645812164,15.9707636829835));
#142425=CARTESIAN_POINT('Ctrl Pts',(19.8658481843313,16.9148032123474,15.974933464691));
#142426=CARTESIAN_POINT('Ctrl Pts',(19.7903801947207,16.8776033053207,15.9791075706661));
#142427=CARTESIAN_POINT('Ctrl Pts',(19.71311106918,16.8441449617549,15.9832816766412));
#142428=CARTESIAN_POINT('Ctrl Pts',(19.6344495075874,16.8145879560715,15.9874557826163));
#142429=CARTESIAN_POINT('Ctrl Pts',(19.5557465188748,16.7850153841878,15.9916320868848));
#142430=CARTESIAN_POINT('Ctrl Pts',(19.4756500721021,16.7593483824272,15.9958083911533));
#142431=CARTESIAN_POINT('Ctrl Pts',(19.3945840932351,16.7376968128099,15.9999846954218));
#142432=CARTESIAN_POINT('Ctrl Pts',(19.3133757562407,16.7160072213621,16.0041683336036));
#142433=CARTESIAN_POINT('Ctrl Pts',(19.2311949364436,16.6983472448517,16.0083519717853));
#142434=CARTESIAN_POINT('Ctrl Pts',(19.1484756398584,16.684775555505,16.012535609967));
#142435=CARTESIAN_POINT('Ctrl Pts',(19.0812407848784,16.6737443862044,16.0159361019689));
#142436=CARTESIAN_POINT('Ctrl Pts',(19.0136504336294,16.6654131890496,16.0193365939707));
#142437=CARTESIAN_POINT('Ctrl Pts',(18.9459382820314,16.6597880988421,16.0227370859726));
#142438=CARTESIAN_POINT('Ctrl Pts',(18.862611928595,16.6528658811356,16.0269217203656));
#142439=CARTESIAN_POINT('Ctrl Pts',(18.7787910168741,16.6500174172728,16.0311063547587));
#142440=CARTESIAN_POINT('Ctrl Pts',(18.6949078655888,16.6512984929826,16.0352909891517));
#142441=CARTESIAN_POINT('Ctrl Pts',(18.6111441115869,16.6525777452396,16.0394696672357));
#142442=CARTESIAN_POINT('Ctrl Pts',(18.5273187500338,16.6579748547684,16.0436483453196));
#142443=CARTESIAN_POINT('Ctrl Pts',(18.4438686393698,16.6674937991861,16.0478270234035));
#142444=CARTESIAN_POINT('Ctrl Pts',(18.3589227454464,16.6771833638414,16.052080601289));
#142445=CARTESIAN_POINT('Ctrl Pts',(18.2743661679611,16.691144024519,16.0563341791744));
#142446=CARTESIAN_POINT('Ctrl Pts',(18.1906591204417,16.709324423791,16.0605877570599));
#142447=CARTESIAN_POINT('Ctrl Pts',(18.1085748973793,16.7271523605469,16.0647588710378));
#142448=CARTESIAN_POINT('Ctrl Pts',(18.0273080288931,16.7490377781068,16.0689299850158));
#142449=CARTESIAN_POINT('Ctrl Pts',(17.9472849642524,16.7748802466774,16.0731010989937));
#142450=CARTESIAN_POINT('Ctrl Pts',(17.8672887521237,16.8007140435581,16.0772708133141));
#142451=CARTESIAN_POINT('Ctrl Pts',(17.7885359523436,16.8305021131094,16.0814405276345));
#142452=CARTESIAN_POINT('Ctrl Pts',(17.7114383592366,16.8640940174691,16.0856102419549));
#142453=CARTESIAN_POINT('Ctrl Pts',(17.6343435095929,16.8976847264847,16.0897798078989));
#142454=CARTESIAN_POINT('Ctrl Pts',(17.5589041709148,16.9350788166487,16.093949373843));
#142455=CARTESIAN_POINT('Ctrl Pts',(17.4855113682725,16.9760780469002,16.098118939787));
#142456=CARTESIAN_POINT('Ctrl Pts',(17.4095381652293,17.0185187595094,16.1024351025259));
#142457=CARTESIAN_POINT('Ctrl Pts',(17.3357585487127,17.0648225852953,16.1067512652648));
#142458=CARTESIAN_POINT('Ctrl Pts',(17.2645758959968,17.1147192929919,16.1110674280038));
#142459=CARTESIAN_POINT('Ctrl Pts',(17.1957120107061,17.1629906206834,16.1152429921954));
#142460=CARTESIAN_POINT('Ctrl Pts',(17.1292788382186,17.214624022349,16.1194185563871));
#142461=CARTESIAN_POINT('Ctrl Pts',(17.0656083164574,17.2693333987819,16.1235941205788));
#142462=CARTESIAN_POINT('Ctrl Pts',(16.9987219480044,17.3268060157592,16.1279805825913));
#142463=CARTESIAN_POINT('Ctrl Pts',(16.934885070269,17.3876731058187,16.1323670446039));
#142464=CARTESIAN_POINT('Ctrl Pts',(16.8744375629657,17.4515604464003,16.1367535066164));
#142465=CARTESIAN_POINT('Ctrl Pts',(16.8139900556624,17.5154477869819,16.141139968629));
#142466=CARTESIAN_POINT('Ctrl Pts',(16.7569322374058,17.5823548872471,16.1455264306415));
#142467=CARTESIAN_POINT('Ctrl Pts',(16.703552701499,17.6518708302357,16.149912892654));
#142468=CARTESIAN_POINT('Ctrl Pts',(16.652554439824,17.7182856499019,16.1541036735168));
#142469=CARTESIAN_POINT('Ctrl Pts',(16.6047208600205,17.7873320135743,16.1582944543796));
#142470=CARTESIAN_POINT('Ctrl Pts',(16.5603345705064,17.8586765917043,16.1624852352424));
#142471=CARTESIAN_POINT('Ctrl Pts',(16.5160108372518,17.9299206196422,16.1666701097864));
#142472=CARTESIAN_POINT('Ctrl Pts',(16.4751249866853,18.0034560458725,16.1708549843304));
#142473=CARTESIAN_POINT('Ctrl Pts',(16.4379187528239,18.0789174471946,16.1750398588744));
#142474=CARTESIAN_POINT('Ctrl Pts',(16.4007539244062,18.15429487031,16.1792200762261));
#142475=CARTESIAN_POINT('Ctrl Pts',(16.367260780246,18.2315936031771,16.1834002935778));
#142476=CARTESIAN_POINT('Ctrl Pts',(16.3376364602561,18.3104214163183,16.1875805109295));
#142477=CARTESIAN_POINT('Ctrl Pts',(16.3080359860438,18.3891857778597,16.1917573634602));
#142478=CARTESIAN_POINT('Ctrl Pts',(16.2822983085872,18.4694763469326,16.1959342159909));
#142479=CARTESIAN_POINT('Ctrl Pts',(16.2605729619713,18.5508797931071,16.2001110685216));
#142480=CARTESIAN_POINT('Ctrl Pts',(16.238858101653,18.632243947813,16.2042859049869));
#142481=CARTESIAN_POINT('Ctrl Pts',(16.2211518401951,18.7147194701818,16.2084607414522));
#142482=CARTESIAN_POINT('Ctrl Pts',(16.2075538451844,18.7978779516685,16.2126355779176));
#142483=CARTESIAN_POINT('Ctrl Pts',(16.1939550163504,18.8810415323988,16.2168106703821));
#142484=CARTESIAN_POINT('Ctrl Pts',(16.1844650395064,18.964887705472,16.2209857628467));
#142485=CARTESIAN_POINT('Ctrl Pts',(16.1791322578277,19.048978951962,16.2251608553112));
#142486=CARTESIAN_POINT('Ctrl Pts',(16.1756711337435,19.1035565169223,16.227870606798));
#142487=CARTESIAN_POINT('Ctrl Pts',(16.1739601228212,19.158237148325,16.2305803582847));
#142488=CARTESIAN_POINT('Ctrl Pts',(16.174000705501,19.2129005695108,16.2332901097715));
#142489=CARTESIAN_POINT('',(16.1740005630998,19.2093020392336,16.1667098902285));
#142490=CARTESIAN_POINT('Ctrl Pts',(20.2954006413529,17.1784744524704,15.8832287081017));
#142491=CARTESIAN_POINT('Ctrl Pts',(20.2230158542988,17.1219688498783,15.8878110837942));
#142492=CARTESIAN_POINT('Ctrl Pts',(19.4492534959823,16.5850864470858,15.9347853950472));
#142493=CARTESIAN_POINT('Ctrl Pts',(17.4141947910433,16.4867742032747,16.0241516418607));
#142494=CARTESIAN_POINT('Ctrl Pts',(16.2227678179363,18.1548349051303,16.1140629935438));
#142495=CARTESIAN_POINT('Ctrl Pts',(16.1704458861955,19.106523168223,16.1615824096664));
#142496=CARTESIAN_POINT('Ctrl Pts',(16.1712324881214,19.2093002032634,16.1667098902285));
#142497=CARTESIAN_POINT('Ctrl Pts',(16.1740005630998,19.2093020392336,16.1667098902285));
#142498=CARTESIAN_POINT('Ctrl Pts',(16.1739457994085,19.2918687402816,16.1708335669039));
#142499=CARTESIAN_POINT('Ctrl Pts',(16.1778897355288,19.3745927743499,16.1749572435793));
#142500=CARTESIAN_POINT('Ctrl Pts',(16.185851592152,19.4570481489095,16.1790809202548));
#142501=CARTESIAN_POINT('Ctrl Pts',(16.193849980064,19.5398818524496,16.1832235175451));
#142502=CARTESIAN_POINT('Ctrl Pts',(16.2059033176551,19.6224439445466,16.1873661148355));
#142503=CARTESIAN_POINT('Ctrl Pts',(16.2219780566694,19.7043008779901,16.1915087121259));
#142504=CARTESIAN_POINT('Ctrl Pts',(16.23794569149,19.7856124078128,16.1956237077524));
#142505=CARTESIAN_POINT('Ctrl Pts',(16.2578812222445,19.8662276743518,16.1997387033789));
#142506=CARTESIAN_POINT('Ctrl Pts',(16.2816998746989,19.9457272251988,16.2038536990054));
#142507=CARTESIAN_POINT('Ctrl Pts',(16.3055083094403,20.0251926723702,16.2079669293832));
#142508=CARTESIAN_POINT('Ctrl Pts',(16.33319642467,20.1035429002386,16.2120801597611));
#142509=CARTESIAN_POINT('Ctrl Pts',(16.3646289972004,20.1803714721883,16.2161933901389));
#142510=CARTESIAN_POINT('Ctrl Pts',(16.3960581246075,20.2571916234494,16.2203061696919));
#142511=CARTESIAN_POINT('Ctrl Pts',(16.4312307139715,20.3324900117992,16.2244189492448));
#142512=CARTESIAN_POINT('Ctrl Pts',(16.469963164482,20.405879578626,16.2285317287978));
#142513=CARTESIAN_POINT('Ctrl Pts',(16.5091807554344,20.48018838104,16.2326960226666));
#142514=CARTESIAN_POINT('Ctrl Pts',(16.5520477937182,20.552539761255,16.2368603165354));
#142515=CARTESIAN_POINT('Ctrl Pts',(16.5983263505016,20.6225587351713,16.2410246104042));
#142516=CARTESIAN_POINT('Ctrl Pts',(16.6440925485817,20.6918025157112,16.2451428005837));
#142517=CARTESIAN_POINT('Ctrl Pts',(16.6931947649456,20.7587649302322,16.2492609907631));
#142518=CARTESIAN_POINT('Ctrl Pts',(16.7453611252724,20.8231152024351,16.2533791809425));
#142519=CARTESIAN_POINT('Ctrl Pts',(16.7984034996618,20.8885460894828,16.257566526656));
#142520=CARTESIAN_POINT('Ctrl Pts',(16.8546135316783,20.9512759179513,16.2617538723695));
#142521=CARTESIAN_POINT('Ctrl Pts',(16.9136665630956,21.010996160687,16.265941218083));
#142522=CARTESIAN_POINT('Ctrl Pts',(16.972719594513,21.0707164034227,16.2701285637965));
#142523=CARTESIAN_POINT('Ctrl Pts',(17.0346152026565,21.1274267716985,16.2743159095101));
#142524=CARTESIAN_POINT('Ctrl Pts',(17.0989955289249,21.1808630357374,16.2785032552236));
#142525=CARTESIAN_POINT('Ctrl Pts',(17.1633341687151,21.2342646996152,16.2826878896166));
#142526=CARTESIAN_POINT('Ctrl Pts',(17.2304115572045,21.2846103343966,16.2868725240096));
#142527=CARTESIAN_POINT('Ctrl Pts',(17.29990527078,21.3316065895454,16.2910571584027));
#142528=CARTESIAN_POINT('Ctrl Pts',(17.3693000686558,21.378535951342,16.2952358364866));
#142529=CARTESIAN_POINT('Ctrl Pts',(17.4411039821925,21.4221251476138,16.2994145145706));
#142530=CARTESIAN_POINT('Ctrl Pts',(17.5149611920068,21.4621206952553,16.3035931926545));
#142531=CARTESIAN_POINT('Ctrl Pts',(17.5901422392269,21.5028331343439,16.30784677054));
#142532=CARTESIAN_POINT('Ctrl Pts',(17.6674505464319,21.5398215173808,16.3121003484254));
#142533=CARTESIAN_POINT('Ctrl Pts',(17.7464794551571,21.5728643427414,16.3163539263108));
#142534=CARTESIAN_POINT('Ctrl Pts',(17.8239762342744,21.6052665684546,16.3205250402888));
#142535=CARTESIAN_POINT('Ctrl Pts',(17.9031270518499,21.6338746703221,16.3246961542667));
#142536=CARTESIAN_POINT('Ctrl Pts',(17.983524818815,21.6585267112792,16.3288672682447));
#142537=CARTESIAN_POINT('Ctrl Pts',(18.0638956075329,21.6831704800059,16.3330369825651));
#142538=CARTESIAN_POINT('Ctrl Pts',(18.1455120751846,21.7038606894987,16.3372066968854));
#142539=CARTESIAN_POINT('Ctrl Pts',(18.2279505020329,21.7204847888774,16.3413764112058));
#142540=CARTESIAN_POINT('Ctrl Pts',(18.3103859953682,21.7371082966994,16.3455459771499));
#142541=CARTESIAN_POINT('Ctrl Pts',(18.3936429386223,21.7496658919856,16.3497155430939));
#142542=CARTESIAN_POINT('Ctrl Pts',(18.4772872562561,21.758096104822,16.353885109038));
#142543=CARTESIAN_POINT('Ctrl Pts',(18.5638724049115,21.7668227135419,16.3582012717769));
#142544=CARTESIAN_POINT('Ctrl Pts',(18.6508721501767,21.7711262492444,16.3625174345158));
#142545=CARTESIAN_POINT('Ctrl Pts',(18.7378010569183,21.7709971781169,16.3668335972547));
#142546=CARTESIAN_POINT('Ctrl Pts',(18.821898263666,21.7708723114677,16.3710091614464));
#142547=CARTESIAN_POINT('Ctrl Pts',(18.9059287081101,21.7665992585964,16.3751847256381));
#142548=CARTESIAN_POINT('Ctrl Pts',(18.9894564259429,21.7582224116564,16.3793602898298));
#142549=CARTESIAN_POINT('Ctrl Pts',(19.0772029302352,21.7494224700914,16.3837467518423));
#142550=CARTESIAN_POINT('Ctrl Pts',(19.1643940106307,21.7360933624401,16.3881332138548));
#142551=CARTESIAN_POINT('Ctrl Pts',(19.2505367177894,21.7183471676605,16.3925196758674));
#142552=CARTESIAN_POINT('Ctrl Pts',(19.3366794249481,21.700600972881,16.3969061378799));
#142553=CARTESIAN_POINT('Ctrl Pts',(19.4217732165569,21.6784379108237,16.4012925998925));
#142554=CARTESIAN_POINT('Ctrl Pts',(19.5053461655911,21.652029514944,16.405679061905));
#142555=CARTESIAN_POINT('Ctrl Pts',(19.5850737993555,21.6268362085053,16.4098636962981));
#142556=CARTESIAN_POINT('Ctrl Pts',(19.6637142290032,21.5976858772393,16.4140483306911));
#142557=CARTESIAN_POINT('Ctrl Pts',(19.7408462713707,21.5646908432984,16.4182329650842));
#142558=CARTESIAN_POINT('Ctrl Pts',(19.817868525823,21.5317427737044,16.4224116431681));
#142559=CARTESIAN_POINT('Ctrl Pts',(19.8933862382763,21.4949610508431,16.4265903212521));
#142560=CARTESIAN_POINT('Ctrl Pts',(19.96699367127,21.4545076569087,16.430768999336));
#142561=CARTESIAN_POINT('Ctrl Pts',(20.0419204645992,21.4133291649615,16.4350225772215));
#142562=CARTESIAN_POINT('Ctrl Pts',(20.1148673616167,21.3683462231047,16.4392761551069));
#142563=CARTESIAN_POINT('Ctrl Pts',(20.1854279979956,21.3197808721237,16.4435297329923));
#142564=CARTESIAN_POINT('Ctrl Pts',(20.2546206787505,21.2721570552389,16.4477008469703));
#142565=CARTESIAN_POINT('Ctrl Pts',(20.3215184014305,21.2210887664917,16.4518719609482));
#142566=CARTESIAN_POINT('Ctrl Pts',(20.3857646529993,21.1668306499036,16.4560430749262));
#142567=CARTESIAN_POINT('Ctrl Pts',(20.4499893461179,21.1125907401505,16.4602127892466));
#142568=CARTESIAN_POINT('Ctrl Pts',(20.5115639839658,21.055163424919,16.4643825035669));
#142569=CARTESIAN_POINT('Ctrl Pts',(20.5701645776071,20.9948440637962,16.4685522178873));
#142570=CARTESIAN_POINT('Ctrl Pts',(20.6287630859878,20.9345268490952,16.4727217838314));
#142571=CARTESIAN_POINT('Ctrl Pts',(20.6843874406314,20.8713181236703,16.4768913497754));
#142572=CARTESIAN_POINT('Ctrl Pts',(20.7367509982118,20.8055496038573,16.4810609157195));
#142573=CARTESIAN_POINT('Ctrl Pts',(20.7909555938794,20.7374687440219,16.4853770784584));
#142574=CARTESIAN_POINT('Ctrl Pts',(20.8416654983873,20.6666451485148,16.4896932411973));
#142575=CARTESIAN_POINT('Ctrl Pts',(20.888609938477,20.5934818309896,16.4940094039362));
#142576=CARTESIAN_POINT('Ctrl Pts',(20.9340251683684,20.5227018008373,16.4981849681279));
#142577=CARTESIAN_POINT('Ctrl Pts',(20.9759162929432,20.4497325726915,16.5023605323196));
#142578=CARTESIAN_POINT('Ctrl Pts',(21.0140846597658,20.3749647521729,16.5065360965113));
#142579=CARTESIAN_POINT('Ctrl Pts',(21.0541808200599,20.2964205867835,16.5109225585238));
#142580=CARTESIAN_POINT('Ctrl Pts',(21.0901680280105,20.2158918932934,16.5153090205363));
#142581=CARTESIAN_POINT('Ctrl Pts',(21.1218737001564,20.133853830301,16.5196954825489));
#142582=CARTESIAN_POINT('Ctrl Pts',(21.1535793723023,20.0518157673086,16.5240819445614));
#142583=CARTESIAN_POINT('Ctrl Pts',(21.1810033999592,19.9682689098143,16.5284684065739));
#142584=CARTESIAN_POINT('Ctrl Pts',(21.2040345704695,19.8837029215676,16.5328548685865));
#142585=CARTESIAN_POINT('Ctrl Pts',(21.2260060426842,19.8030279397969,16.5370395029795));
#142586=CARTESIAN_POINT('Ctrl Pts',(21.244061800264,19.7211252621464,16.5412241373726));
#142587=CARTESIAN_POINT('Ctrl Pts',(21.2580683099057,19.6384098348539,16.5454087717656));
#142588=CARTESIAN_POINT('Ctrl Pts',(21.2720548830145,19.5558121427341,16.5495874498496));
#142589=CARTESIAN_POINT('Ctrl Pts',(21.2820035803663,19.4724044485339,16.5537661279335));
#142590=CARTESIAN_POINT('Ctrl Pts',(21.28783098536,19.3886155911379,16.5579448060175));
#142591=CARTESIAN_POINT('Ctrl Pts',(21.2937628424001,19.3033248786909,16.5621983839029));
#142592=CARTESIAN_POINT('Ctrl Pts',(21.2954240788116,19.2176396691378,16.5664519617883));
#142593=CARTESIAN_POINT('Ctrl Pts',(21.2927814384536,19.1320218370346,16.5707055396738));
#142594=CARTESIAN_POINT('Ctrl Pts',(21.2901900308356,19.0480638736762,16.5748766536517));
#142595=CARTESIAN_POINT('Ctrl Pts',(21.2834601502021,18.9641711795844,16.5790477676297));
#142596=CARTESIAN_POINT('Ctrl Pts',(21.2726129381323,18.8807813597822,16.5832188816076));
#142597=CARTESIAN_POINT('Ctrl Pts',(21.2617693659493,18.7974195222394,16.587388595928));
#142598=CARTESIAN_POINT('Ctrl Pts',(21.246811265521,18.7145606796674,16.5915583102484));
#142599=CARTESIAN_POINT('Ctrl Pts',(21.2278116184524,18.6326371280314,16.5957280245688));
#142600=CARTESIAN_POINT('Ctrl Pts',(21.2088126474729,18.5507164915871,16.5998975905128));
#142601=CARTESIAN_POINT('Ctrl Pts',(21.1857725205575,18.4697315278525,16.6040671564568));
#142602=CARTESIAN_POINT('Ctrl Pts',(21.1588150040536,18.3901028102639,16.6082367224009));
#142603=CARTESIAN_POINT('Ctrl Pts',(21.130909694525,18.3076744451973,16.6125528851398));
#142604=CARTESIAN_POINT('Ctrl Pts',(21.0988065683012,18.2266999715503,16.6168690478787));
#142605=CARTESIAN_POINT('Ctrl Pts',(21.0626979316574,18.1476252104292,16.6211852106176));
#142606=CARTESIAN_POINT('Ctrl Pts',(21.0277655300543,18.0711263013345,16.6253607748093));
#142607=CARTESIAN_POINT('Ctrl Pts',(20.9890848280187,17.9964056357569,16.629536339001));
#142608=CARTESIAN_POINT('Ctrl Pts',(20.9468767362674,17.9238416763713,16.6337119031927));
#142609=CARTESIAN_POINT('Ctrl Pts',(20.9025368141419,17.8476126839014,16.6380983652052));
#142610=CARTESIAN_POINT('Ctrl Pts',(20.854304119971,17.7737644826753,16.6424848272177));
#142611=CARTESIAN_POINT('Ctrl Pts',(20.8024847707863,17.7026993824091,16.6468712892303));
#142612=CARTESIAN_POINT('Ctrl Pts',(20.7506654216016,17.6316342821429,16.6512577512428));
#142613=CARTESIAN_POINT('Ctrl Pts',(20.6952598420585,17.5633526854597,16.6556442132554));
#142614=CARTESIAN_POINT('Ctrl Pts',(20.6366195645773,17.4982131503051,16.6600306752679));
#142615=CARTESIAN_POINT('Ctrl Pts',(20.5806916320437,17.4360865764914,16.6642142460496));
#142616=CARTESIAN_POINT('Ctrl Pts',(20.5216135032554,17.3765866334633,16.6683978168312));
#142617=CARTESIAN_POINT('Ctrl Pts',(20.459661587099,17.320049951265,16.6725813876129));
#142618=CARTESIAN_POINT('Ctrl Pts',(20.40634711204,17.2713957090722,16.6761816778691));
#142619=CARTESIAN_POINT('Ctrl Pts',(20.3509051344092,17.2249357340853,16.6797819681254));
#142620=CARTESIAN_POINT('Ctrl Pts',(20.2935357313021,17.1808649545431,16.6833822583817));
#142621=CARTESIAN_POINT('Origin',(18.734,19.211,-1.76670989022852));
#142622=CARTESIAN_POINT('',(20.2961055602205,17.1775141780511,17.5498940766593));
#142623=CARTESIAN_POINT('',(20.2910030380574,17.1841723135106,17.4833253062578));
#142624=CARTESIAN_POINT('',(20.2935357313021,17.1808649545432,-1.76670989022852));
#142625=CARTESIAN_POINT('',(16.1737370555978,19.211835565301,17.0332901097715));
#142626=CARTESIAN_POINT('Ctrl Pts',(16.1700998775752,19.2118367523274,17.0332901097715));
#142627=CARTESIAN_POINT('Ctrl Pts',(16.1699051698649,19.2575742435185,17.0355745863224));
#142628=CARTESIAN_POINT('Ctrl Pts',(16.1917620114795,20.1518505208751,17.0802509984337));
#142629=CARTESIAN_POINT('Ctrl Pts',(17.2348044634258,21.8407724883182,17.1673193461055));
#142630=CARTESIAN_POINT('Ctrl Pts',(20.1337363827015,21.8950321637681,17.2944951527869));
#142631=CARTESIAN_POINT('Ctrl Pts',(21.7484970482859,19.4868589187841,17.4216709594684));
#142632=CARTESIAN_POINT('Ctrl Pts',(20.978102385576,17.7053825246215,17.5068039340925));
#142633=CARTESIAN_POINT('Ctrl Pts',(20.301649822008,17.1817662346287,17.5495449731561));
#142634=CARTESIAN_POINT('Ctrl Pts',(20.2961055602205,17.1775141780511,17.5498940766593));
#142635=CARTESIAN_POINT('Ctrl Pts',(20.2935357313021,17.1808649545432,16.7498176665395));
#142636=CARTESIAN_POINT('Ctrl Pts',(20.226858468591,17.1296439414898,16.7539938197931));
#142637=CARTESIAN_POINT('Ctrl Pts',(20.1577087704231,17.0817524478804,16.7581699730466));
#142638=CARTESIAN_POINT('Ctrl Pts',(20.0864599566968,17.0374195286276,16.7623461263002));
#142639=CARTESIAN_POINT('Ctrl Pts',(20.0150847693762,16.9930079763412,16.7665296867718));
#142640=CARTESIAN_POINT('Ctrl Pts',(19.9416034309245,16.952167832392,16.7707132472434));
#142641=CARTESIAN_POINT('Ctrl Pts',(19.8664139286561,16.9150821673706,16.7748968077149));
#142642=CARTESIAN_POINT('Ctrl Pts',(19.8011426897056,16.8828884803502,16.7785285138304));
#142643=CARTESIAN_POINT('Ctrl Pts',(19.7345847399538,16.8535234039901,16.7821602199458));
#142644=CARTESIAN_POINT('Ctrl Pts',(19.6670104728629,16.8270764572814,16.7857919260613));
#142645=CARTESIAN_POINT('Ctrl Pts',(19.5891480046,16.7966029554973,16.7899765604543));
#142646=CARTESIAN_POINT('Ctrl Pts',(19.5096461031212,16.7698914102528,16.7941611948473));
#142647=CARTESIAN_POINT('Ctrl Pts',(19.4289030536308,16.7471189667408,16.7983458292404));
#142648=CARTESIAN_POINT('Ctrl Pts',(19.3482749318773,16.7243789369834,16.8025245073243));
#142649=CARTESIAN_POINT('Ctrl Pts',(19.2664096101499,16.7055669958483,16.8067031854083));
#142650=CARTESIAN_POINT('Ctrl Pts',(19.1837245465113,16.6908119450594,16.8108818634922));
#142651=CARTESIAN_POINT('Ctrl Pts',(19.0995574125318,16.6757924205894,16.8151354413777));
#142652=CARTESIAN_POINT('Ctrl Pts',(19.0145413088147,16.66497683224,16.8193890192631));
#142653=CARTESIAN_POINT('Ctrl Pts',(18.929131904193,16.6584476420716,16.8236425971485));
#142654=CARTESIAN_POINT('Ctrl Pts',(18.8453783275426,16.6520450329952,16.8278137111265));
#142655=CARTESIAN_POINT('Ctrl Pts',(18.7612470435307,16.6497641415373,16.8319848251044));
#142656=CARTESIAN_POINT('Ctrl Pts',(18.6771754083917,16.6516307484483,16.8361559390824));
#142657=CARTESIAN_POINT('Ctrl Pts',(18.5931319843017,16.6534967290012,16.8403256534028));
#142658=CARTESIAN_POINT('Ctrl Pts',(18.5091486288698,16.6595074337161,16.8444953677231));
#142659=CARTESIAN_POINT('Ctrl Pts',(18.4256629639196,16.6696365328468,16.8486650820435));
#142660=CARTESIAN_POINT('Ctrl Pts',(18.3421802697477,16.6797652715406,16.8528346479875));
#142661=CARTESIAN_POINT('Ctrl Pts',(18.2591956874269,16.6940120570168,16.8570042139316));
#142662=CARTESIAN_POINT('Ctrl Pts',(18.1771406148226,16.7122988123547,16.8611737798756));
#142663=CARTESIAN_POINT('Ctrl Pts',(18.0922005870915,16.7312285074512,16.8654899426145));
#142664=CARTESIAN_POINT('Ctrl Pts',(18.008257163138,16.7544874341396,16.8698061053535));
#142665=CARTESIAN_POINT('Ctrl Pts',(17.9257741739148,16.781932068869,16.8741222680924));
#142666=CARTESIAN_POINT('Ctrl Pts',(17.8459780593899,16.8084826975088,16.878297832284));
#142667=CARTESIAN_POINT('Ctrl Pts',(17.7675491154086,16.838950308513,16.8824733964757));
#142668=CARTESIAN_POINT('Ctrl Pts',(17.6908872600139,16.8731557340835,16.8866489606674));
#142669=CARTESIAN_POINT('Ctrl Pts',(17.6103533965496,16.9090887943838,16.8910354226799));
#142670=CARTESIAN_POINT('Ctrl Pts',(17.5317703445184,16.9491469214588,16.8954218846925));
#142671=CARTESIAN_POINT('Ctrl Pts',(17.4555708448952,16.9930687802869,16.899808346705));
#142672=CARTESIAN_POINT('Ctrl Pts',(17.3793713452719,17.0369906391151,16.9041948087175));
#142673=CARTESIAN_POINT('Ctrl Pts',(17.3055558437866,17.0847758505362,16.9085812707301));
#142674=CARTESIAN_POINT('Ctrl Pts',(17.2345184376722,17.1361132454423,16.9129677327426));
#142675=CARTESIAN_POINT('Ctrl Pts',(17.167299168743,17.1846913445463,16.9171184300414));
#142676=CARTESIAN_POINT('Ctrl Pts',(17.1023079512147,17.2366370916662,16.9212691273401));
#142677=CARTESIAN_POINT('Ctrl Pts',(17.0399060592653,17.2917173944502,16.9254198246388));
#142678=CARTESIAN_POINT('Ctrl Pts',(16.9775932241692,17.3467190893861,16.9295645982704));
#142679=CARTESIAN_POINT('Ctrl Pts',(16.9178627255451,17.4048461509352,16.9337093719019));
#142680=CARTESIAN_POINT('Ctrl Pts',(16.8610458812396,17.4658229691466,16.9378541455334));
#142681=CARTESIAN_POINT('Ctrl Pts',(16.8042942087153,17.5267298438772,16.9419941649009));
#142682=CARTESIAN_POINT('Ctrl Pts',(16.7504498675423,17.5904796396564,16.9461341842684));
#142683=CARTESIAN_POINT('Ctrl Pts',(16.6998090154256,17.6567583719781,16.9502742036359));
#142684=CARTESIAN_POINT('Ctrl Pts',(16.6491995836851,17.7229959813207,16.9544116543072));
#142685=CARTESIAN_POINT('Ctrl Pts',(16.6017899801563,17.7917590422704,16.9585491049784));
#142686=CARTESIAN_POINT('Ctrl Pts',(16.5578367768805,17.8626997269368,16.9626865556497));
#142687=CARTESIAN_POINT('Ctrl Pts',(16.5138971231854,17.9336185425139,16.9668227308571));
#142688=CARTESIAN_POINT('Ctrl Pts',(16.473412000563,18.0067132510728,16.9709589060645));
#142689=CARTESIAN_POINT('Ctrl Pts',(16.436594403761,18.0816074524907,16.9750950812719));
#142690=CARTESIAN_POINT('Ctrl Pts',(16.3997766632185,18.1565019463048,16.9792312726275));
#142691=CARTESIAN_POINT('Ctrl Pts',(16.3666266817619,18.2331955257885,16.983367463983));
#142692=CARTESIAN_POINT('Ctrl Pts',(16.3373106052885,18.3112889656799,16.9875036553386));
#142693=CARTESIAN_POINT('Ctrl Pts',(16.3079666664254,18.3894566266172,16.9916437777855));
#142694=CARTESIAN_POINT('Ctrl Pts',(16.2824640727846,18.4690263650884,16.9957839002324));
#142695=CARTESIAN_POINT('Ctrl Pts',(16.2609198329123,18.5495814584111,16.9999240226793));
#142696=CARTESIAN_POINT('Ctrl Pts',(16.2393648184701,18.6301768384414,17.0040662156583));
#142697=CARTESIAN_POINT('Ctrl Pts',(16.2217721969232,18.711758096276,17.0082084086373));
#142698=CARTESIAN_POINT('Ctrl Pts',(16.2082078057625,18.7938983438913,17.0123506016163));
#142699=CARTESIAN_POINT('Ctrl Pts',(16.194621013815,18.8761742412484,17.016499635181));
#142700=CARTESIAN_POINT('Ctrl Pts',(16.1850757885661,18.9590105062903,17.0206486687458));
#142701=CARTESIAN_POINT('Ctrl Pts',(16.1795860271471,19.0419755778186,17.0247977023105));
#142702=CARTESIAN_POINT('Ctrl Pts',(16.1758404729028,19.0985809841505,17.0276285047975));
#142703=CARTESIAN_POINT('Ctrl Pts',(16.1739816679355,19.1552463005709,17.0304593072845));
#142704=CARTESIAN_POINT('Ctrl Pts',(16.1740001363332,19.2118354794422,17.0332901097715));
#142705=CARTESIAN_POINT('',(16.1741505176752,19.209803254934,16.9667098397549));
#142706=CARTESIAN_POINT('Ctrl Pts',(20.2935357313021,17.1808649545431,16.6833822583817));
#142707=CARTESIAN_POINT('Ctrl Pts',(20.2246022413362,17.1279107232836,16.687708267697));
#142708=CARTESIAN_POINT('Ctrl Pts',(20.1528852221898,17.0784073718384,16.6920342770124));
#142709=CARTESIAN_POINT('Ctrl Pts',(20.0787694878185,17.0326531440948,16.6963602863277));
#142710=CARTESIAN_POINT('Ctrl Pts',(20.0073031354739,16.988534472278,16.7005316557217));
#142711=CARTESIAN_POINT('Ctrl Pts',(19.9336070721956,16.9479017083688,16.7047030251158));
#142712=CARTESIAN_POINT('Ctrl Pts',(19.8580574417036,16.9109793766684,16.7088743945098));
#142713=CARTESIAN_POINT('Ctrl Pts',(19.7825359166057,16.8740707805306,16.7130442121031));
#142714=CARTESIAN_POINT('Ctrl Pts',(19.7051626065606,16.8408700772147,16.7172140296963));
#142715=CARTESIAN_POINT('Ctrl Pts',(19.6263379519364,16.8115556935961,16.7213838472895));
#142716=CARTESIAN_POINT('Ctrl Pts',(19.5475189755514,16.7822434216783,16.7255533645043));
#142717=CARTESIAN_POINT('Ctrl Pts',(19.4672492937651,16.7568170727964,16.7297228817192));
#142718=CARTESIAN_POINT('Ctrl Pts',(19.3859477207409,16.7354062996079,16.733892398934));
#142719=CARTESIAN_POINT('Ctrl Pts',(19.3046276162901,16.7139906461674,16.7380628665253));
#142720=CARTESIAN_POINT('Ctrl Pts',(19.2222755986575,16.6965925017586,16.7422333341166));
#142721=CARTESIAN_POINT('Ctrl Pts',(19.1393226393413,16.6832908478155,16.7464038017079));
#142722=CARTESIAN_POINT('Ctrl Pts',(19.0562756193694,16.6699741110796,16.7505789982072));
#142723=CARTESIAN_POINT('Ctrl Pts',(18.9726267529364,16.6607632053402,16.7547541947066));
#142724=CARTESIAN_POINT('Ctrl Pts',(18.8888135568868,16.6556853887233,16.7589293912059));
#142725=CARTESIAN_POINT('Ctrl Pts',(18.8049436062157,16.6506041336317,16.7631074149653));
#142726=CARTESIAN_POINT('Ctrl Pts',(18.7209095638014,16.6496615421292,16.7672854387246));
#142727=CARTESIAN_POINT('Ctrl Pts',(18.6371480049381,16.6528327476389,16.771463462484));
#142728=CARTESIAN_POINT('Ctrl Pts',(18.5532533714703,16.6560089913419,16.7756481240001));
#142729=CARTESIAN_POINT('Ctrl Pts',(18.4696325420907,16.6633120309538,16.7798327855163));
#142730=CARTESIAN_POINT('Ctrl Pts',(18.3867154598213,16.6746653517028,16.7840174470325));
#142731=CARTESIAN_POINT('Ctrl Pts',(18.3656523886079,16.677549387138,16.7850804586714));
#142732=CARTESIAN_POINT('Ctrl Pts',(18.3446346664914,16.68069452864,16.7861434703104));
#142733=CARTESIAN_POINT('Ctrl Pts',(18.3236691980735,16.6840990060965,16.7872064819493));
#142734=CARTESIAN_POINT('Ctrl Pts',(18.2411368748191,16.6975010168866,16.7913911163424));
#142735=CARTESIAN_POINT('Ctrl Pts',(18.1591082470636,16.7149756618514,16.7955757507354));
#142736=CARTESIAN_POINT('Ctrl Pts',(18.078016311923,16.7364726914061,16.7997603851285));
#142737=CARTESIAN_POINT('Ctrl Pts',(17.9970398011148,16.7579391226001,16.8039390632124));
#142738=CARTESIAN_POINT('Ctrl Pts',(17.9169977755058,16.7834164491321,16.8081177412964));
#142739=CARTESIAN_POINT('Ctrl Pts',(17.8383151283773,16.8128030500507,16.8122964193803));
#142740=CARTESIAN_POINT('Ctrl Pts',(17.7582221513472,16.8427163846709,16.8165499972657));
#142741=CARTESIAN_POINT('Ctrl Pts',(17.679538241764,16.8766804423687,16.8208035751512));
#142742=CARTESIAN_POINT('Ctrl Pts',(17.6026975961517,16.9145342652138,16.8250571530366));
#142743=CARTESIAN_POINT('Ctrl Pts',(17.5273466563967,16.9516542178374,16.8292282670146));
#142744=CARTESIAN_POINT('Ctrl Pts',(17.4537685795461,16.9925142474789,16.8333993809925));
#142745=CARTESIAN_POINT('Ctrl Pts',(17.3823529481856,17.0369139282629,16.8375704949705));
#142746=CARTESIAN_POINT('Ctrl Pts',(17.31096128103,17.081298710305,16.8417402092909));
#142747=CARTESIAN_POINT('Ctrl Pts',(17.2417310086119,17.1292205418818,16.8459099236112));
#142748=CARTESIAN_POINT('Ctrl Pts',(17.1750254175662,17.1804340071484,16.8500796379316));
#142749=CARTESIAN_POINT('Ctrl Pts',(17.1083222001916,17.2316456500202,16.8542492038756));
#142750=CARTESIAN_POINT('Ctrl Pts',(17.0441438499409,17.2861484128722,16.8584187698197));
#142751=CARTESIAN_POINT('Ctrl Pts',(16.9828219564696,17.3436555058434,16.8625883357637));
#142752=CARTESIAN_POINT('Ctrl Pts',(16.9193440608726,17.4031844772607,16.8669044985027));
#142753=CARTESIAN_POINT('Ctrl Pts',(16.8589276101184,17.465932613281,16.8712206612416));
#142754=CARTESIAN_POINT('Ctrl Pts',(16.8018987983272,17.5315402813719,16.8755368239805));
#142755=CARTESIAN_POINT('Ctrl Pts',(16.7467276940818,17.5950107865753,16.8797123881722));
#142756=CARTESIAN_POINT('Ctrl Pts',(16.6947271674386,17.6611569867925,16.8838879523639));
#142757=CARTESIAN_POINT('Ctrl Pts',(16.6461502555165,17.7296211003055,16.8880635165556));
#142758=CARTESIAN_POINT('Ctrl Pts',(16.5951198392538,17.8015431734341,16.8924499785681));
#142759=CARTESIAN_POINT('Ctrl Pts',(16.5478682932595,17.8760229761491,16.8968364405806));
#142760=CARTESIAN_POINT('Ctrl Pts',(16.5046350837973,17.9526152931617,16.9012229025932));
#142761=CARTESIAN_POINT('Ctrl Pts',(16.461401874335,18.0292076101744,16.9056093646057));
#142762=CARTESIAN_POINT('Ctrl Pts',(16.4221871920777,18.1079118882384,16.9099958266183));
#142763=CARTESIAN_POINT('Ctrl Pts',(16.3871718743353,18.1882596866316,16.9143822886308));
#142764=CARTESIAN_POINT('Ctrl Pts',(16.3503471043862,18.272759539339,16.9189954255354));
#142765=CARTESIAN_POINT('Ctrl Pts',(16.3180481684135,18.3593459986726,16.9236085624399));
#142766=CARTESIAN_POINT('Ctrl Pts',(16.2904920397068,18.4475415217682,16.9282216993445));
#142767=CARTESIAN_POINT('Ctrl Pts',(16.2630147812854,18.5354846144106,16.9328216326736));
#142768=CARTESIAN_POINT('Ctrl Pts',(16.240253377301,18.6250273148911,16.9374215660027));
#142769=CARTESIAN_POINT('Ctrl Pts',(16.2223767943066,18.7156729639699,16.9420214993319));
#142770=CARTESIAN_POINT('Ctrl Pts',(16.2045882581335,18.8058721596483,16.9465987767929));
#142771=CARTESIAN_POINT('Ctrl Pts',(16.1916366671697,18.8971631896627,16.9511760542538));
#142772=CARTESIAN_POINT('Ctrl Pts',(16.1836406660146,18.9890376888893,16.9557533317148));
#142773=CARTESIAN_POINT('Ctrl Pts',(16.1772607284144,19.0623435277384,16.9594055003442));
#142774=CARTESIAN_POINT('Ctrl Pts',(16.174034774907,19.1360203999197,16.9630576689737));
#142775=CARTESIAN_POINT('Ctrl Pts',(16.1740002797795,19.2098031412859,16.9667098376031));
#142776=CARTESIAN_POINT('Ctrl Pts',(16.1776746320478,19.209805920766,16.9667098902285));
#142777=CARTESIAN_POINT('Ctrl Pts',(16.1797896414426,19.7131225343252,16.9916592919231));
#142778=CARTESIAN_POINT('Ctrl Pts',(16.5671403882425,21.07463612297,17.0590006291781));
#142779=CARTESIAN_POINT('Ctrl Pts',(18.7821183121777,22.2377105261597,17.1687339019936));
#142780=CARTESIAN_POINT('Ctrl Pts',(21.3050300949207,20.8088411160513,17.2959097086751));
#142781=CARTESIAN_POINT('Ctrl Pts',(21.4403822833153,18.4219199310893,17.4007735100965));
#142782=CARTESIAN_POINT('Ctrl Pts',(20.61274935573,17.4306044799469,17.4632453759574));
#142783=CARTESIAN_POINT('Ctrl Pts',(20.2910030380574,17.1841723135106,17.4833253062578));
#142784=CARTESIAN_POINT('Origin',(18.734,19.211,-1.76670989022852));
#142785=CARTESIAN_POINT('',(20.2935357313021,17.1808649545432,18.3499540490682));
#142786=CARTESIAN_POINT('',(20.2935357313021,17.1808649545431,18.283231856284));
#142787=CARTESIAN_POINT('',(20.2935357313021,17.1808649545432,-1.76670989022852));
#142788=CARTESIAN_POINT('',(16.1740010840393,19.2086440968075,17.8332901097715));
#142789=CARTESIAN_POINT('Ctrl Pts',(16.1740010840393,19.2086440968075,17.8332901097715));
#142790=CARTESIAN_POINT('Ctrl Pts',(16.1739248258781,19.2915086264566,17.837412174938));
#142791=CARTESIAN_POINT('Ctrl Pts',(16.177876160498,19.3744847533445,17.8415342401044));
#142792=CARTESIAN_POINT('Ctrl Pts',(16.1858608731257,19.4571442465142,17.8456563052709));
#142793=CARTESIAN_POINT('Ctrl Pts',(16.1938402258665,19.5397482529614,17.8497756034244));
#142794=CARTESIAN_POINT('Ctrl Pts',(16.205847540348,19.6220355783689,17.853894901578));
#142795=CARTESIAN_POINT('Ctrl Pts',(16.2218365582967,19.7035797825425,17.8580141997315));
#142796=CARTESIAN_POINT('Ctrl Pts',(16.2378199266111,19.7850951735058,17.862132042353));
#142797=CARTESIAN_POINT('Ctrl Pts',(16.2577821151893,19.8658675009388,17.8662498849745));
#142798=CARTESIAN_POINT('Ctrl Pts',(16.2816254461127,19.9454787590162,17.8703677275959));
#142799=CARTESIAN_POINT('Ctrl Pts',(16.3054679320359,20.0250871956956,17.8744854242824));
#142800=CARTESIAN_POINT('Ctrl Pts',(16.3331911499574,20.1035341923719,17.8786031209688));
#142801=CARTESIAN_POINT('Ctrl Pts',(16.364647494651,20.1804166830608,17.8827208176552));
#142802=CARTESIAN_POINT('Ctrl Pts',(16.396133878009,20.257372591286,17.8868424464612));
#142803=CARTESIAN_POINT('Ctrl Pts',(16.4313603282317,20.3327605713697,17.8909640752672));
#142804=CARTESIAN_POINT('Ctrl Pts',(16.4701312380089,20.4061979871474,17.8950857040732));
#142805=CARTESIAN_POINT('Ctrl Pts',(16.5089205032735,20.479670170733,17.8992092842006));
#142806=CARTESIAN_POINT('Ctrl Pts',(16.5512573267502,20.5511895451374,17.903332864328));
#142807=CARTESIAN_POINT('Ctrl Pts',(16.5969016205558,20.6204007650689,17.9074564444553));
#142808=CARTESIAN_POINT('Ctrl Pts',(16.6426258760309,20.6897332322415,17.9115872484507));
#142809=CARTESIAN_POINT('Ctrl Pts',(16.6916688941171,20.7567490876318,17.915718052446));
#142810=CARTESIAN_POINT('Ctrl Pts',(16.743749207993,20.8211247730892,17.9198488564413));
#142811=CARTESIAN_POINT('Ctrl Pts',(16.7879829276106,20.8758014024869,17.9233572996922));
#142812=CARTESIAN_POINT('Ctrl Pts',(16.8344068718463,20.9285739549632,17.9268657429432));
#142813=CARTESIAN_POINT('Ctrl Pts',(16.8828286089276,20.979265953095,17.9303741861941));
#142814=CARTESIAN_POINT('Ctrl Pts',(16.9405827898753,21.039727948248,17.9345588205871));
#142815=CARTESIAN_POINT('Ctrl Pts',(17.0014097311532,21.0974699797563,17.9387434549801));
#142816=CARTESIAN_POINT('Ctrl Pts',(17.0650229727701,21.152163486824,17.9429280893731));
#142817=CARTESIAN_POINT('Ctrl Pts',(17.1285456688113,21.2067791444541,17.947106767457));
#142818=CARTESIAN_POINT('Ctrl Pts',(17.1948464417153,21.2583545993042,17.9512854455409));
#142819=CARTESIAN_POINT('Ctrl Pts',(17.2636010628233,21.3065970427421,17.9554641236248));
#142820=CARTESIAN_POINT('Ctrl Pts',(17.3335880611026,21.3557041973082,17.9597177015102));
#142821=CARTESIAN_POINT('Ctrl Pts',(17.4061174102899,21.4013573280785,17.9639712793957));
#142822=CARTESIAN_POINT('Ctrl Pts',(17.4808106950311,21.4432895345164,17.9682248572811));
#142823=CARTESIAN_POINT('Ctrl Pts',(17.5540559046944,21.4844088033079,17.972395971259));
#142824=CARTESIAN_POINT('Ctrl Pts',(17.6293814748144,21.5219498994727,17.9765670852369));
#142825=CARTESIAN_POINT('Ctrl Pts',(17.706401696316,21.5557050403549,17.9807381992148));
#142826=CARTESIAN_POINT('Ctrl Pts',(17.7833960729387,21.5894488543737,17.9849079135351));
#142827=CARTESIAN_POINT('Ctrl Pts',(17.8620835505882,21.6194090516659,17.9890776278554));
#142828=CARTESIAN_POINT('Ctrl Pts',(17.9420562076477,21.6454249895519,17.9932473421757));
#142829=CARTESIAN_POINT('Ctrl Pts',(18.0220260189367,21.6714400016791,17.9974169081197));
#142830=CARTESIAN_POINT('Ctrl Pts',(18.1032804809775,21.6935108919569,18.0015864740637));
#142831=CARTESIAN_POINT('Ctrl Pts',(18.1853954972942,21.7115265644682,18.0057560400077));
#142832=CARTESIAN_POINT('Ctrl Pts',(18.2703975762872,21.7301756458007,18.0100722027467));
#142833=CARTESIAN_POINT('Ctrl Pts',(18.3563213344853,21.7444789277004,18.0143883654857));
#142834=CARTESIAN_POINT('Ctrl Pts',(18.4426856715114,21.7543709839536,18.0187045282247));
#142835=CARTESIAN_POINT('Ctrl Pts',(18.5262366993405,21.7639408075146,18.0228800924163));
#142836=CARTESIAN_POINT('Ctrl Pts',(18.6101995699748,21.7693824000208,18.0270556566079));
#142837=CARTESIAN_POINT('Ctrl Pts',(18.6941361080731,21.7706896042529,18.0312312207995));
#142838=CARTESIAN_POINT('Ctrl Pts',(18.7823120811743,21.7720628322632,18.0356176828122));
#142839=CARTESIAN_POINT('Ctrl Pts',(18.870458408217,21.7688730610124,18.0400041448249));
#142840=CARTESIAN_POINT('Ctrl Pts',(18.9580725064404,21.7611748002554,18.0443906068375));
#142841=CARTESIAN_POINT('Ctrl Pts',(19.0456866046639,21.7534765394983,18.0487770688502));
#142842=CARTESIAN_POINT('Ctrl Pts',(19.132767910028,21.7412699451077,18.0531635308629));
#142843=CARTESIAN_POINT('Ctrl Pts',(19.2188278686568,21.7246710082614,18.0575499928755));
#142844=CARTESIAN_POINT('Ctrl Pts',(19.3009280810131,21.7088358131057,18.0617346272685));
#142845=CARTESIAN_POINT('Ctrl Pts',(19.3824044612751,21.6889446480546,18.0659192616614));
#142846=CARTESIAN_POINT('Ctrl Pts',(19.4628256864492,21.6650605369004,18.0701038960543));
#142847=CARTESIAN_POINT('Ctrl Pts',(19.5431324419635,21.6412104218221,18.0742825741382));
#142848=CARTESIAN_POINT('Ctrl Pts',(19.6223865883777,21.6133787796397,18.078461252222));
#142849=CARTESIAN_POINT('Ctrl Pts',(19.7001664211467,21.5816797435859,18.0826399303058));
#142850=CARTESIAN_POINT('Ctrl Pts',(19.7793404015215,21.5494125250915,18.0868935081913));
#142851=CARTESIAN_POINT('Ctrl Pts',(19.8569862208222,21.5131379942492,18.0911470860767));
#142852=CARTESIAN_POINT('Ctrl Pts',(19.9326746288814,21.4730298702882,18.0954006639622));
#142853=CARTESIAN_POINT('Ctrl Pts',(20.0068956694542,21.433699320576,18.09957177794));
#142854=CARTESIAN_POINT('Ctrl Pts',(20.0792340927642,21.3906827199666,18.1037428919179));
#142855=CARTESIAN_POINT('Ctrl Pts',(20.1493064094734,21.3441919199415,18.1079140058957));
#142856=CARTESIAN_POINT('Ctrl Pts',(20.2193552127399,21.2977167203534,18.112083720216));
#142857=CARTESIAN_POINT('Ctrl Pts',(20.2871390365835,21.2477698907686,18.1162534345363));
#142858=CARTESIAN_POINT('Ctrl Pts',(20.3523020056983,21.1946074758765,18.1204231488565));
#142859=CARTESIAN_POINT('Ctrl Pts',(20.4174626560349,21.1414469527312,18.1245927148004));
#142860=CARTESIAN_POINT('Ctrl Pts',(20.4800022811539,21.0850713632533,18.1287622807444));
#142861=CARTESIAN_POINT('Ctrl Pts',(20.5395979115911,21.0257771713513,18.1329318466883));
#142862=CARTESIAN_POINT('Ctrl Pts',(20.6012888508791,20.9643982688056,18.1372480094273));
#142863=CARTESIAN_POINT('Ctrl Pts',(20.6598245480544,20.8998920810988,18.1415641721664));
#142864=CARTESIAN_POINT('Ctrl Pts',(20.7148895795158,20.8326277235438,18.1458803349055));
#142865=CARTESIAN_POINT('Ctrl Pts',(20.768160873366,20.767554495365,18.150055899097));
#142866=CARTESIAN_POINT('Ctrl Pts',(20.8181839009053,20.6999004393907,18.1542314632886));
#142867=CARTESIAN_POINT('Ctrl Pts',(20.864716308885,20.6300306589541,18.1584070274802));
#142868=CARTESIAN_POINT('Ctrl Pts',(20.9135989581756,20.5566319220009,18.162793489493));
#142869=CARTESIAN_POINT('Ctrl Pts',(20.9586288003486,20.4807882477351,18.1671799515058));
#142870=CARTESIAN_POINT('Ctrl Pts',(20.9995796309652,20.4029517338197,18.1715664135186));
#142871=CARTESIAN_POINT('Ctrl Pts',(21.0405304615817,20.3251152199043,18.1759528755314));
#142872=CARTESIAN_POINT('Ctrl Pts',(21.0774021064019,20.2452864249786,18.1803393375442));
#142873=CARTESIAN_POINT('Ctrl Pts',(21.1100276507034,20.1639389293617,18.184725799557));
#142874=CARTESIAN_POINT('Ctrl Pts',(21.1411520453503,20.0863343526005,18.1889104339505));
#142875=CARTESIAN_POINT('Ctrl Pts',(21.1685283427045,20.00705890033,18.193095068344));
#142876=CARTESIAN_POINT('Ctrl Pts',(21.1919760688457,19.926509360513,18.1972797027374));
#142877=CARTESIAN_POINT('Ctrl Pts',(21.2153904200511,19.8460744729959,18.2014583808218));
#142878=CARTESIAN_POINT('Ctrl Pts',(21.2348871797096,19.7643695380469,18.2056370589062));
#142879=CARTESIAN_POINT('Ctrl Pts',(21.2503340551361,19.6818109206067,18.2098157369906));
#142880=CARTESIAN_POINT('Ctrl Pts',(21.266057804701,19.5977724992938,18.2140693148759));
#142881=CARTESIAN_POINT('Ctrl Pts',(21.2775848741471,19.5128499374387,18.2183228927613));
#142882=CARTESIAN_POINT('Ctrl Pts',(21.2848289888802,19.4274981974254,18.2225764706466));
#142883=CARTESIAN_POINT('Ctrl Pts',(21.2919326623144,19.3438011674314,18.226747584625));
#142884=CARTESIAN_POINT('Ctrl Pts',(21.2949179252555,19.2596919311857,18.2309186986034));
#142885=CARTESIAN_POINT('Ctrl Pts',(21.2937553357682,19.1756076137221,18.2350898125818));
#142886=CARTESIAN_POINT('Ctrl Pts',(21.2925931363989,19.0915515115633,18.2392595269026));
#142887=CARTESIAN_POINT('Ctrl Pts',(21.287285855196,19.0075207711861,18.2434292412234));
#142888=CARTESIAN_POINT('Ctrl Pts',(21.2778561566697,18.9239532195383,18.2475989555442));
#142889=CARTESIAN_POINT('Ctrl Pts',(21.2684267936926,18.8403886415826,18.2517685214887));
#142890=CARTESIAN_POINT('Ctrl Pts',(21.2548753574853,18.7572876766216,18.2559380874331));
#142891=CARTESIAN_POINT('Ctrl Pts',(21.2372763100334,18.6750823611546,18.2601076533776));
#142892=CARTESIAN_POINT('Ctrl Pts',(21.2190585017879,18.5899868082262,18.264423816116));
#142893=CARTESIAN_POINT('Ctrl Pts',(21.1965032689153,18.5058515744424,18.2687399788544));
#142894=CARTESIAN_POINT('Ctrl Pts',(21.1697502461669,18.4231416762528,18.2730561415928));
#142895=CARTESIAN_POINT('Ctrl Pts',(21.1438687003149,18.3431260442794,18.2772317057849));
#142896=CARTESIAN_POINT('Ctrl Pts',(21.114058861765,18.2644447370881,18.281407269977));
#142897=CARTESIAN_POINT('Ctrl Pts',(21.0804965434245,18.1874991589174,18.2855828341691));
#142898=CARTESIAN_POINT('Ctrl Pts',(21.045239072183,18.1066672425405,18.2899692961807));
#142899=CARTESIAN_POINT('Ctrl Pts',(21.0058403441653,18.0277515290332,18.2943557581922));
#142900=CARTESIAN_POINT('Ctrl Pts',(20.9625580617871,17.9511869324206,18.2987422202038));
#142901=CARTESIAN_POINT('Ctrl Pts',(20.9192757794088,17.8746223358079,18.3031286822153));
#142902=CARTESIAN_POINT('Ctrl Pts',(20.8721103180847,17.8004093049791,18.3075151442269));
#142903=CARTESIAN_POINT('Ctrl Pts',(20.8213695361433,17.7289445288449,18.3119016062384));
#142904=CARTESIAN_POINT('Ctrl Pts',(20.7729692668539,17.6607761980217,18.3160857345562));
#142905=CARTESIAN_POINT('Ctrl Pts',(20.7211361130899,17.5948544666328,18.320269862874));
#142906=CARTESIAN_POINT('Ctrl Pts',(20.6661059353023,17.5315457270977,18.3244539911917));
#142907=CARTESIAN_POINT('Ctrl Pts',(20.6102092780632,17.4672401577484,18.3287040008378));
#142908=CARTESIAN_POINT('Ctrl Pts',(20.551014254789,17.4056310123225,18.3329540104839));
#142909=CARTESIAN_POINT('Ctrl Pts',(20.4888142269941,17.3470721503397,18.33720402013));
#142910=CARTESIAN_POINT('Ctrl Pts',(20.4266141991991,17.2885132883569,18.3414540297761));
#142911=CARTESIAN_POINT('Ctrl Pts',(20.3614094818074,17.2330051012627,18.3457040394221));
#142912=CARTESIAN_POINT('Ctrl Pts',(20.2935357313021,17.1808649545432,18.3499540490682));
#142913=CARTESIAN_POINT('Ctrl Pts',(20.2961055602205,17.1775141780511,17.5498940766593));
#142914=CARTESIAN_POINT('Ctrl Pts',(19.6284053936389,16.6654353848825,17.5919369087166));
#142915=CARTESIAN_POINT('Ctrl Pts',(17.7316712639343,16.3587002035979,17.6763716763344));
#142916=CARTESIAN_POINT('Ctrl Pts',(16.286227466659,17.9552740380232,17.7708370079901));
#142917=CARTESIAN_POINT('Ctrl Pts',(16.1722336618266,19.0070072559387,17.8232595075886));
#142918=CARTESIAN_POINT('Ctrl Pts',(16.1740883584118,19.2086434103328,17.8332900716265));
#142919=CARTESIAN_POINT('',(16.1740009581142,19.2132148462219,17.7667099127475));
#142920=CARTESIAN_POINT('Ctrl Pts',(20.2910030380574,17.1841723135106,17.4833253062578));
#142921=CARTESIAN_POINT('Ctrl Pts',(19.9334915614287,16.9103468713152,17.5056373115179));
#142922=CARTESIAN_POINT('Ctrl Pts',(18.6971962548141,16.3747766224752,17.5703412523384));
#142923=CARTESIAN_POINT('Ctrl Pts',(16.6895185666654,17.1540155201862,17.6648027803286));
#142924=CARTESIAN_POINT('Ctrl Pts',(16.1805385807744,18.6141143559075,17.7369523030588));
#142925=CARTESIAN_POINT('Ctrl Pts',(16.1756125809373,19.2132129985223,17.7667098902285));
#142926=CARTESIAN_POINT('Ctrl Pts',(16.1740009581142,19.2132148462218,17.7667099127475));
#142927=CARTESIAN_POINT('Ctrl Pts',(16.1740887027227,19.3146332252549,17.7717442924629));
#142928=CARTESIAN_POINT('Ctrl Pts',(16.1802070184511,19.4157876786429,17.7767786721782));
#142929=CARTESIAN_POINT('Ctrl Pts',(16.1922394471755,19.5160463769745,17.7818130518935));
#142930=CARTESIAN_POINT('Ctrl Pts',(16.2044426849033,19.6177283198346,17.7869188982596));
#142931=CARTESIAN_POINT('Ctrl Pts',(16.2227290670649,19.71848890314,17.7920247446257));
#142932=CARTESIAN_POINT('Ctrl Pts',(16.2469282568518,19.8176911441861,17.7971305909918));
#142933=CARTESIAN_POINT('Ctrl Pts',(16.2587491290717,19.8661496680319,17.7996247057948));
#142934=CARTESIAN_POINT('Ctrl Pts',(16.2719801580739,19.9142366801005,17.8021188205978));
#142935=CARTESIAN_POINT('Ctrl Pts',(16.2865973915759,19.9618797988219,17.8046129354008));
#142936=CARTESIAN_POINT('Ctrl Pts',(16.3111222362101,20.0418155872439,17.8087975697939));
#142937=CARTESIAN_POINT('Ctrl Pts',(16.3396130703746,20.1206973427815,17.8129822041869));
#142938=CARTESIAN_POINT('Ctrl Pts',(16.3719611025222,20.1981029565358,17.8171668385799));
#142939=CARTESIAN_POINT('Ctrl Pts',(16.4042630912499,20.2753983929799,17.8213455166639));
#142940=CARTESIAN_POINT('Ctrl Pts',(16.440411196743,20.351221440268,17.8255241947478));
#142941=CARTESIAN_POINT('Ctrl Pts',(16.480246839823,20.4251650188471,17.8297028728317));
#142942=CARTESIAN_POINT('Ctrl Pts',(16.5207965081758,20.5004339829301,17.8339564507172));
#142943=CARTESIAN_POINT('Ctrl Pts',(16.5651670712162,20.5737549756816,17.8382100286026));
#142944=CARTESIAN_POINT('Ctrl Pts',(16.6131398985284,20.6447197878197,17.8424636064881));
#142945=CARTESIAN_POINT('Ctrl Pts',(16.6601826789718,20.7143088085979,17.846634720466));
#142946=CARTESIAN_POINT('Ctrl Pts',(16.7106890267626,20.7816317931436,17.8508058344439));
#142947=CARTESIAN_POINT('Ctrl Pts',(16.7644072919754,20.8463301087231,17.8549769484219));
#142948=CARTESIAN_POINT('Ctrl Pts',(16.8181075315056,20.9110067141581,17.8591466627423));
#142949=CARTESIAN_POINT('Ctrl Pts',(16.875017254325,20.9730600461346,17.8633163770626));
#142950=CARTESIAN_POINT('Ctrl Pts',(16.934843824038,21.032163653958,17.867486091383));
#142951=CARTESIAN_POINT('Ctrl Pts',(16.9946682648649,21.0912651586214,17.871655657327));
#142952=CARTESIAN_POINT('Ctrl Pts',(17.0574090183537,21.147416825124,17.8758252232711));
#142953=CARTESIAN_POINT('Ctrl Pts',(17.1227367799309,21.2003292426476,17.8799947892151));
#142954=CARTESIAN_POINT('Ctrl Pts',(17.1903613850149,21.2551019954968,17.884310951954));
#142955=CARTESIAN_POINT('Ctrl Pts',(17.2607578915088,21.3064031452814,17.888627114693));
#142956=CARTESIAN_POINT('Ctrl Pts',(17.333525567137,21.3539585537049,17.8929432774319));
#142957=CARTESIAN_POINT('Ctrl Pts',(17.4039228433852,21.3999648497009,17.8971188416236));
#142958=CARTESIAN_POINT('Ctrl Pts',(17.4765387490622,21.4424654946024,17.9012944058152));
#142959=CARTESIAN_POINT('Ctrl Pts',(17.5509843556048,21.4812585723032,17.9054699700069));
#142960=CARTESIAN_POINT('Ctrl Pts',(17.6291900327565,21.5220109961371,17.9098564320195));
#142961=CARTESIAN_POINT('Ctrl Pts',(17.7094145736836,21.558671228602,17.914242894032));
#142962=CARTESIAN_POINT('Ctrl Pts',(17.7911842815277,21.5910627136699,17.9186293560446));
#142963=CARTESIAN_POINT('Ctrl Pts',(17.8729539893717,21.6234541987377,17.9230158180571));
#142964=CARTESIAN_POINT('Ctrl Pts',(17.9562682900627,21.6515768229132,17.9274022800697));
#142965=CARTESIAN_POINT('Ctrl Pts',(18.0406384682269,21.6753152773656,17.9317887420822));
#142966=CARTESIAN_POINT('Ctrl Pts',(18.1211266494267,21.6979614903396,17.9359733764753));
#142967=CARTESIAN_POINT('Ctrl Pts',(18.2028752706869,21.716702405741,17.9401580108683));
#142968=CARTESIAN_POINT('Ctrl Pts',(18.2854705184225,21.7314010205037,17.9443426452613));
#142969=CARTESIAN_POINT('Ctrl Pts',(18.3679482020463,21.7460787136075,17.9485213233452));
#142970=CARTESIAN_POINT('Ctrl Pts',(18.4512696694583,21.7567254548487,17.9527000014292));
#142971=CARTESIAN_POINT('Ctrl Pts',(18.5350067952745,21.7632542397796,17.9568786795131));
#142972=CARTESIAN_POINT('Ctrl Pts',(18.6202448488907,21.7699000484884,17.9611322573985));
#142973=CARTESIAN_POINT('Ctrl Pts',(18.7059131447156,21.7722786894991,17.965385835284));
#142974=CARTESIAN_POINT('Ctrl Pts',(18.7915501028463,21.7703530404503,17.9696394131694));
#142975=CARTESIAN_POINT('Ctrl Pts',(18.8755268214362,21.768464723866,17.9738105271473));
#142976=CARTESIAN_POINT('Ctrl Pts',(18.9594729254761,21.76243753283,17.9779816411253));
#142977=CARTESIAN_POINT('Ctrl Pts',(19.04295064826,21.7522889440085,17.9821527551032));
#142978=CARTESIAN_POINT('Ctrl Pts',(19.1264003592878,21.742143760644,17.9863224694236));
#142979=CARTESIAN_POINT('Ctrl Pts',(19.209381544911,21.7278799815763,17.9904921837439));
#142980=CARTESIAN_POINT('Ctrl Pts',(19.2914613132264,21.709566966134,17.9946618980643));
#142981=CARTESIAN_POINT('Ctrl Pts',(19.3735381607915,21.6912546023473,17.9988314640083));
#142982=CARTESIAN_POINT('Ctrl Pts',(19.454713206017,21.6688933896802,18.0030010299523));
#142983=CARTESIAN_POINT('Ctrl Pts',(19.5345648538852,21.6426035685785,18.0071705958964));
#142984=CARTESIAN_POINT('Ctrl Pts',(19.6172239871857,21.6153894297986,18.0114867586353));
#142985=CARTESIAN_POINT('Ctrl Pts',(19.6984644293619,21.5839654477009,18.0158029213742));
#142986=CARTESIAN_POINT('Ctrl Pts',(19.7778387647094,21.5485201888519,18.0201190841132));
#142987=CARTESIAN_POINT('Ctrl Pts',(19.8546274894308,21.514229555582,18.0242946483049));
#142988=CARTESIAN_POINT('Ctrl Pts',(19.9296694183931,21.4761758636208,18.0284702124965));
#142989=CARTESIAN_POINT('Ctrl Pts',(20.0025842524506,21.434576846982,18.0326457766882));
#142990=CARTESIAN_POINT('Ctrl Pts',(20.079181841439,21.3908767629043,18.0370322387008));
#142991=CARTESIAN_POINT('Ctrl Pts',(20.1534313177603,21.34326410831,18.0414187007134));
#142992=CARTESIAN_POINT('Ctrl Pts',(20.2249278226102,21.2920416208636,18.045805162726));
#142993=CARTESIAN_POINT('Ctrl Pts',(20.2964243274601,21.2408191334172,18.0501916247385));
#142994=CARTESIAN_POINT('Ctrl Pts',(20.365167454674,21.1859872343881,18.0545780867511));
#142995=CARTESIAN_POINT('Ctrl Pts',(20.4307957154104,21.1278944415812,18.0589645487637));
#142996=CARTESIAN_POINT('Ctrl Pts',(20.4934043225861,21.0724745842854,18.0631491831568));
#142997=CARTESIAN_POINT('Ctrl Pts',(20.5534114448285,21.0138810328615,18.0673338175499));
#142998=CARTESIAN_POINT('Ctrl Pts',(20.6104778947951,20.9523875818856,18.071518451943));
#142999=CARTESIAN_POINT('Ctrl Pts',(20.6674631177336,20.8909816592258,18.0756971300271));
#143000=CARTESIAN_POINT('Ctrl Pts',(20.7215156722283,20.8266843701415,18.0798758081111));
#143001=CARTESIAN_POINT('Ctrl Pts',(20.7723306651574,20.7598086064711,18.0840544861951));
#143002=CARTESIAN_POINT('Ctrl Pts',(20.8240564803137,20.6917341428009,18.0883080640805));
#143003=CARTESIAN_POINT('Ctrl Pts',(20.8724271646773,20.6209881765789,18.0925616419659));
#143004=CARTESIAN_POINT('Ctrl Pts',(20.91716165977,20.5479387298266,18.0968152198513));
#143005=CARTESIAN_POINT('Ctrl Pts',(20.9610288893839,20.4763054891425,18.1009863338293));
#143006=CARTESIAN_POINT('Ctrl Pts',(21.0013994094997,20.4024576962095,18.1051574478073));
#143007=CARTESIAN_POINT('Ctrl Pts',(21.0380509604128,20.326772903337,18.1093285617853));
#143008=CARTESIAN_POINT('Ctrl Pts',(21.0746902125439,20.2511135072276,18.1134982761058));
#143009=CARTESIAN_POINT('Ctrl Pts',(21.1076127735552,20.173618749099,18.1176679904262));
#143010=CARTESIAN_POINT('Ctrl Pts',(21.136642647489,20.094690165424,18.1218377047466));
#143011=CARTESIAN_POINT('Ctrl Pts',(21.1656714884152,20.0157643903668,18.1260072706907));
#143012=CARTESIAN_POINT('Ctrl Pts',(21.1908077596747,19.9354053232572,18.1301768366348));
#143013=CARTESIAN_POINT('Ctrl Pts',(21.211924363067,19.8540325426592,18.1343464025789));
#143014=CARTESIAN_POINT('Ctrl Pts',(21.2337834001838,19.7697987954823,18.1386625653178));
#143015=CARTESIAN_POINT('Ctrl Pts',(21.2513347146947,19.6844792346863,18.1429787280566));
#143016=CARTESIAN_POINT('Ctrl Pts',(21.2644946836059,19.5985521335795,18.1472948907955));
#143017=CARTESIAN_POINT('Ctrl Pts',(21.2772259679145,19.5154240987508,18.1514704549872));
#143018=CARTESIAN_POINT('Ctrl Pts',(21.2858476079666,19.4317279704214,18.1556460191789));
#143019=CARTESIAN_POINT('Ctrl Pts',(21.290336834896,19.3479013752813,18.1598215833707));
#143020=CARTESIAN_POINT('Ctrl Pts',(21.2950528020053,19.2598408981036,18.1642080453831));
#143021=CARTESIAN_POINT('Ctrl Pts',(21.295207927637,19.1716370118692,18.1685945073955));
#143022=CARTESIAN_POINT('Ctrl Pts',(21.2908376238657,19.083794004918,18.1729809694079));
#143023=CARTESIAN_POINT('Ctrl Pts',(21.2864673200944,18.9959509979668,18.1773674314203));
#143024=CARTESIAN_POINT('Ctrl Pts',(21.2775717212916,18.9084694398441,18.1817538934327));
#143025=CARTESIAN_POINT('Ctrl Pts',(21.2642482087237,18.8218419315364,18.1861403554451));
#143026=CARTESIAN_POINT('Ctrl Pts',(21.2515412573717,18.7392232130713,18.1903238287683));
#143027=CARTESIAN_POINT('Ctrl Pts',(21.2347598613936,18.6570738106191,18.1945073020914));
#143028=CARTESIAN_POINT('Ctrl Pts',(21.2139505970127,18.5758267666406,18.1986907754146));
#143029=CARTESIAN_POINT('Ctrl Pts',(21.1931684634965,18.4946856515652,18.2028687943764));
#143030=CARTESIAN_POINT('Ctrl Pts',(21.1683689994549,18.4144450007966,18.2070468133382));
#143031=CARTESIAN_POINT('Ctrl Pts',(21.1396501998692,18.3355303455463,18.2112248323));
#143032=CARTESIAN_POINT('Ctrl Pts',(21.11096022557,18.2566948975601,18.2153986577511));
#143033=CARTESIAN_POINT('Ctrl Pts',(21.078358883834,18.1791832320113,18.2195724832022));
#143034=CARTESIAN_POINT('Ctrl Pts',(21.0419943136825,18.103407002546,18.2237463086533));
#143035=CARTESIAN_POINT('Ctrl Pts',(21.0056553325363,18.0276840952658,18.2279171970687));
#143036=CARTESIAN_POINT('Ctrl Pts',(20.9655585822467,17.9536946114992,18.2320880854841));
#143037=CARTESIAN_POINT('Ctrl Pts',(20.9219002659552,17.8818301740435,18.2362589738995));
#143038=CARTESIAN_POINT('Ctrl Pts',(20.8782487043954,17.8099768553171,18.2404292170029));
#143039=CARTESIAN_POINT('Ctrl Pts',(20.8310368995156,17.7402483290549,18.2445994601063));
#143040=CARTESIAN_POINT('Ctrl Pts',(20.7805064538479,17.6730106195559,18.2487697032098));
#143041=CARTESIAN_POINT('Ctrl Pts',(20.7299824361656,17.6057814633758,18.252939415816));
#143042=CARTESIAN_POINT('Ctrl Pts',(20.6761408980458,17.5410428584497,18.2571091284222));
#143043=CARTESIAN_POINT('Ctrl Pts',(20.6192651021105,17.4791294809472,18.2612788410284));
#143044=CARTESIAN_POINT('Ctrl Pts',(20.5623509460967,17.4171743457517,18.2654513659117));
#143045=CARTESIAN_POINT('Ctrl Pts',(20.502398759404,17.3580485804598,18.2696238907951));
#143046=CARTESIAN_POINT('Ctrl Pts',(20.4397297081047,17.3020510318793,18.2737964156785));
#143047=CARTESIAN_POINT('Ctrl Pts',(20.3924913150559,17.2598414538696,18.276941562547));
#143048=CARTESIAN_POINT('Ctrl Pts',(20.343710066172,17.2194085323209,18.2800867094155));
#143049=CARTESIAN_POINT('Ctrl Pts',(20.2935357313021,17.1808649545431,18.2832318562841));
#143050=CARTESIAN_POINT('Origin',(18.734,19.211,-1.76670989022852));
#143051=CARTESIAN_POINT('',(20.2912840337091,17.1837659559064,19.1498287221711));
#143052=CARTESIAN_POINT('',(20.2935357313021,17.1808649545431,19.0833436983648));
#143053=CARTESIAN_POINT('',(20.2935357313021,17.1808649545432,-1.76670989022852));
#143054=CARTESIAN_POINT('',(16.1743944470979,19.2113823947302,18.633290134885));
#143055=CARTESIAN_POINT('Ctrl Pts',(16.1781629602604,19.2113866753936,18.633290374834));
#143056=CARTESIAN_POINT('Ctrl Pts',(16.1776269335845,19.615981772308,18.6533365919835));
#143057=CARTESIAN_POINT('Ctrl Pts',(16.4590846999913,20.8754715672834,18.7157747446936));
#143058=CARTESIAN_POINT('Ctrl Pts',(18.4329096444066,22.2230815390193,18.8206048329641));
#143059=CARTESIAN_POINT('Ctrl Pts',(21.103709402057,21.094551947962,18.9477806396456));
#143060=CARTESIAN_POINT('Ctrl Pts',(21.532350072377,18.6295872811128,19.0575219360479));
#143061=CARTESIAN_POINT('Ctrl Pts',(20.6891187884342,17.492345631807,19.1248712968897));
#143062=CARTESIAN_POINT('Ctrl Pts',(20.2912840337091,17.1837659559064,19.1498287221711));
#143063=CARTESIAN_POINT('Ctrl Pts',(20.2935357313021,17.1808649545432,18.3499540490682));
#143064=CARTESIAN_POINT('Ctrl Pts',(20.2269224839007,17.129693117609,18.3541251305527));
#143065=CARTESIAN_POINT('Ctrl Pts',(20.157738873817,17.0817655823163,18.3582962120371));
#143066=CARTESIAN_POINT('Ctrl Pts',(20.0863370241469,17.0373430415262,18.3624672935216));
#143067=CARTESIAN_POINT('Ctrl Pts',(20.0149587887766,16.9929351923331,18.3666369955296));
#143068=CARTESIAN_POINT('Ctrl Pts',(19.9413641611146,16.9520302782791,18.3708066975376));
#143069=CARTESIAN_POINT('Ctrl Pts',(19.8659339714226,16.9148455007688,18.3749763995456));
#143070=CARTESIAN_POINT('Ctrl Pts',(19.7905061011064,16.8776618666399,18.379145973341));
#143071=CARTESIAN_POINT('Ctrl Pts',(19.7132431940035,16.844198344213,18.3833155471363));
#143072=CARTESIAN_POINT('Ctrl Pts',(19.6345491545281,16.8146254006774,18.3874851209316));
#143073=CARTESIAN_POINT('Ctrl Pts',(19.5534056519861,16.7841319575277,18.3917844785973));
#143074=CARTESIAN_POINT('Ctrl Pts',(19.4707409318527,16.7577754970438,18.396083836263));
#143075=CARTESIAN_POINT('Ctrl Pts',(19.3870163605659,16.7356879726319,18.4003831939287));
#143076=CARTESIAN_POINT('Ctrl Pts',(19.3057019355853,16.7142362730985,18.4045587876761));
#143077=CARTESIAN_POINT('Ctrl Pts',(19.2233883259854,16.6968110951066,18.4087343814235));
#143078=CARTESIAN_POINT('Ctrl Pts',(19.1405083013071,16.6834812560599,18.4129099751709));
#143079=CARTESIAN_POINT('Ctrl Pts',(19.0539434509894,16.6695587756273,18.4172712147957));
#143080=CARTESIAN_POINT('Ctrl Pts',(18.9667612123123,16.6601043263589,18.4216324544206));
#143081=CARTESIAN_POINT('Ctrl Pts',(18.8794581009856,16.6551357741739,18.4259936940454));
#143082=CARTESIAN_POINT('Ctrl Pts',(18.7921549896588,16.6501672219889,18.4303549336702));
#143083=CARTESIAN_POINT('Ctrl Pts',(18.7047315697535,16.6496844957764,18.434716173295));
#143084=CARTESIAN_POINT('Ctrl Pts',(18.6176794289206,16.6536440363642,18.4390774129198));
#143085=CARTESIAN_POINT('Ctrl Pts',(18.5341524013311,16.6574432382304,18.4432620473123));
#143086=CARTESIAN_POINT('Ctrl Pts',(18.4506562604971,16.6653459878634,18.4474466817047));
#143087=CARTESIAN_POINT('Ctrl Pts',(18.3676269095308,16.6773522820684,18.4516313160972));
#143088=CARTESIAN_POINT('Ctrl Pts',(18.2847157405689,16.6893414867996,18.4558099941805));
#143089=CARTESIAN_POINT('Ctrl Pts',(18.2022704931355,16.7054225689873,18.4599886722639));
#143090=CARTESIAN_POINT('Ctrl Pts',(18.1207249420869,16.725543562373,18.4641673503472));
#143091=CARTESIAN_POINT('Ctrl Pts',(18.0377177456267,16.746025210108,18.4684209282328));
#143092=CARTESIAN_POINT('Ctrl Pts',(17.9556432985583,16.7706930025008,18.4726745061184));
#143093=CARTESIAN_POINT('Ctrl Pts',(17.8749514567222,16.7994371042222,18.476928084004));
#143094=CARTESIAN_POINT('Ctrl Pts',(17.7958239837114,16.8276239454371,18.4810991979813));
#143095=CARTESIAN_POINT('Ctrl Pts',(17.7180264386454,16.8597302905275,18.4852703119587));
#143096=CARTESIAN_POINT('Ctrl Pts',(17.6419689102696,16.8956019566687,18.489441425936));
#143097=CARTESIAN_POINT('Ctrl Pts',(17.5659369037321,16.9314615857259,18.4936111402558));
#143098=CARTESIAN_POINT('Ctrl Pts',(17.4916441700226,16.971083830448,18.4977808545755));
#143099=CARTESIAN_POINT('Ctrl Pts',(17.4194798631979,17.0142667868078,18.5019505688953));
#143100=CARTESIAN_POINT('Ctrl Pts',(17.3473181242892,17.0574482065325,18.5061201348387));
#143101=CARTESIAN_POINT('Ctrl Pts',(17.2772850559937,17.1041898490211,18.5102897007821));
#143102=CARTESIAN_POINT('Ctrl Pts',(17.2097430958426,17.1542450583192,18.5144592667256));
#143103=CARTESIAN_POINT('Ctrl Pts',(17.1398264436724,17.2060601470428,18.5187754294652));
#143104=CARTESIAN_POINT('Ctrl Pts',(17.0725797574077,17.2614258339335,18.5230915922048));
#143105=CARTESIAN_POINT('Ctrl Pts',(17.0083685115614,17.3200224839758,18.5274077549445));
#143106=CARTESIAN_POINT('Ctrl Pts',(16.9462489403142,17.3767103542884,18.5315833191355));
#143107=CARTESIAN_POINT('Ctrl Pts',(16.8869703858411,17.4364215555155,18.5357588833266));
#143108=CARTESIAN_POINT('Ctrl Pts',(16.8308254399579,17.4988298583352,18.5399344475177));
#143109=CARTESIAN_POINT('Ctrl Pts',(16.7718447463028,17.5643902561989,18.5443209095316));
#143110=CARTESIAN_POINT('Ctrl Pts',(16.7163229051916,17.6329269235817,18.5487073715455));
#143111=CARTESIAN_POINT('Ctrl Pts',(16.6645491064847,17.7040252160939,18.5530938335595));
#143112=CARTESIAN_POINT('Ctrl Pts',(16.6127753077779,17.775123508606,18.5574802955734));
#143113=CARTESIAN_POINT('Ctrl Pts',(16.5647498046499,17.8487828986679,18.5618667575873));
#143114=CARTESIAN_POINT('Ctrl Pts',(16.5207062260027,17.924558913131,18.5662532196012));
#143115=CARTESIAN_POINT('Ctrl Pts',(16.4770273612299,17.9997074453442,18.5706033584188));
#143116=CARTESIAN_POINT('Ctrl Pts',(16.4371122169921,18.0771985084612,18.5749534972363));
#143117=CARTESIAN_POINT('Ctrl Pts',(16.4012086273385,18.1566355413635,18.5793036360539));
#143118=CARTESIAN_POINT('Ctrl Pts',(16.3640774712899,18.2387885765663,18.5838025088637));
#143119=CARTESIAN_POINT('Ctrl Pts',(16.3312374248385,18.3230227236652,18.5883013816735));
#143120=CARTESIAN_POINT('Ctrl Pts',(16.3029130373493,18.4088677290933,18.5928002544833));
#143121=CARTESIAN_POINT('Ctrl Pts',(16.2756354411695,18.4915401396801,18.5971328613513));
#143122=CARTESIAN_POINT('Ctrl Pts',(16.2525458055772,18.5757060184788,18.6014654682194));
#143123=CARTESIAN_POINT('Ctrl Pts',(16.2337970621827,18.660922487526,18.6057980750875));
#143124=CARTESIAN_POINT('Ctrl Pts',(16.2150725182344,18.7460289656627,18.6101250897576));
#143125=CARTESIAN_POINT('Ctrl Pts',(16.2006778102744,18.8321829392905,18.6144521044276));
#143126=CARTESIAN_POINT('Ctrl Pts',(16.1907160845812,18.9189265065566,18.6187791190976));
#143127=CARTESIAN_POINT('Ctrl Pts',(16.1807681682272,19.005549826451,18.6231001354883));
#143128=CARTESIAN_POINT('Ctrl Pts',(16.1752410444519,19.0927607071638,18.6274211518791));
#143129=CARTESIAN_POINT('Ctrl Pts',(16.1741865858058,19.1800923227742,18.6317421682699));
#143130=CARTESIAN_POINT('Ctrl Pts',(16.1740606709629,19.190520751334,18.6322581487704));
#143131=CARTESIAN_POINT('Ctrl Pts',(16.1739984722012,19.2009508929684,18.632774129271));
#143132=CARTESIAN_POINT('Ctrl Pts',(16.1740000284928,19.2113819467091,18.6332901097715));
#143133=CARTESIAN_POINT('',(16.1740000028035,19.2111198080496,18.5667098901964));
#143134=CARTESIAN_POINT('Ctrl Pts',(20.2935357313021,17.1808649545431,18.2832318562841));
#143135=CARTESIAN_POINT('Ctrl Pts',(20.2268915890121,17.1296693843687,18.2874094027522));
#143136=CARTESIAN_POINT('Ctrl Pts',(20.157788967903,17.0818088516824,18.2915869492204));
#143137=CARTESIAN_POINT('Ctrl Pts',(20.0866029412604,17.0375085039748,18.2957644956885));
#143138=CARTESIAN_POINT('Ctrl Pts',(20.0153008783135,16.9931359447832,18.2999488517383));
#143139=CARTESIAN_POINT('Ctrl Pts',(19.9419090336255,16.9523353753359,18.304133207788));
#143140=CARTESIAN_POINT('Ctrl Pts',(19.8668262035835,16.9152855594664,18.3083175638377));
#143141=CARTESIAN_POINT('Ctrl Pts',(19.8369284207219,16.9005324215078,18.3099837632673));
#143142=CARTESIAN_POINT('Ctrl Pts',(19.806762721368,16.886373464749,18.3116499626969));
#143143=CARTESIAN_POINT('Ctrl Pts',(19.7763550154481,16.8728177954295,18.3133161621265));
#143144=CARTESIAN_POINT('Ctrl Pts',(19.6999865269337,16.8387729391862,18.3175007965194));
#143145=CARTESIAN_POINT('Ctrl Pts',(19.6218062328668,16.8084101229908,18.3216854309124));
#143146=CARTESIAN_POINT('Ctrl Pts',(19.5422037920521,16.7819247375776,18.3258700653053));
#143147=CARTESIAN_POINT('Ctrl Pts',(19.4627146554591,16.7554770508322,18.3300487433892));
#143148=CARTESIAN_POINT('Ctrl Pts',(19.3818078256877,16.7328959763057,18.334227421473));
#143149=CARTESIAN_POINT('Ctrl Pts',(19.2998943515233,16.7143295005319,18.3384060995568));
#143150=CARTESIAN_POINT('Ctrl Pts',(19.2165126372019,16.6954302340229,18.3426596774423));
#143151=CARTESIAN_POINT('Ctrl Pts',(19.1320882756872,16.6806911015683,18.3469132553277));
#143152=CARTESIAN_POINT('Ctrl Pts',(19.0470726305014,16.6702155683665,18.3511668332132));
#143153=CARTESIAN_POINT('Ctrl Pts',(18.9637051794947,16.6599431238176,18.3553379471911));
#143154=CARTESIAN_POINT('Ctrl Pts',(18.8797696442084,16.6537704962434,18.3595090611689));
#143155=CARTESIAN_POINT('Ctrl Pts',(18.7957017187992,16.6517436826497,18.3636801751467));
#143156=CARTESIAN_POINT('Ctrl Pts',(18.7116620031942,16.649717549173,18.367849889467));
#143157=CARTESIAN_POINT('Ctrl Pts',(18.627490445211,16.6518344778738,18.3720196037873));
#143158=CARTESIAN_POINT('Ctrl Pts',(18.5436254163474,16.6580884234077,18.3761893181075));
#143159=CARTESIAN_POINT('Ctrl Pts',(18.4597633717615,16.6643421463994,18.3803588840515));
#143160=CARTESIAN_POINT('Ctrl Pts',(18.3762082933038,16.6747325584671,18.3845284499954));
#143161=CARTESIAN_POINT('Ctrl Pts',(18.2933947304035,16.6892016344672,18.3886980159393));
#143162=CARTESIAN_POINT('Ctrl Pts',(18.2076695447883,16.7041794253309,18.3930141786784));
#143163=CARTESIAN_POINT('Ctrl Pts',(18.122739507835,16.723527937402,18.3973303414174));
#143164=CARTESIAN_POINT('Ctrl Pts',(18.0390745966233,16.7471252702822,18.4016465041565));
#143165=CARTESIAN_POINT('Ctrl Pts',(17.958135061099,16.7699539225246,18.405822068348));
#143166=CARTESIAN_POINT('Ctrl Pts',(17.8783799255842,16.796758641008,18.4099976325396));
#143167=CARTESIAN_POINT('Ctrl Pts',(17.800216972615,16.8273789609572,18.4141731967312));
#143168=CARTESIAN_POINT('Ctrl Pts',(17.7181061946991,16.8595458404767,18.418559658744));
#143169=CARTESIAN_POINT('Ctrl Pts',(17.6377532005338,16.895923662579,18.4229461207568));
#143170=CARTESIAN_POINT('Ctrl Pts',(17.5596023636775,16.9362714026064,18.4273325827696));
#143171=CARTESIAN_POINT('Ctrl Pts',(17.4814515268212,16.9766191426339,18.4317190447824));
#143172=CARTESIAN_POINT('Ctrl Pts',(17.4055033100763,17.0209364424643,18.4361055067952));
#143173=CARTESIAN_POINT('Ctrl Pts',(17.3321657913463,17.0689307080656,18.4404919688079));
#143174=CARTESIAN_POINT('Ctrl Pts',(17.2622960528831,17.1146555545476,18.4446710160258));
#143175=CARTESIAN_POINT('Ctrl Pts',(17.19453408493,17.1638887348098,18.4488500632436));
#143176=CARTESIAN_POINT('Ctrl Pts',(17.1292545139166,17.2164093339998,18.4530291104615));
#143177=CARTESIAN_POINT('Ctrl Pts',(17.0640679209106,17.2688551278475,18.4572022054423));
#143178=CARTESIAN_POINT('Ctrl Pts',(17.0013570587502,17.3245787540421,18.461375300423));
#143179=CARTESIAN_POINT('Ctrl Pts',(16.9414683281886,17.3833156165374,18.4655483954038));
#143180=CARTESIAN_POINT('Ctrl Pts',(16.8809773183909,17.4426431743496,18.4697634576868));
#143181=CARTESIAN_POINT('Ctrl Pts',(16.8233659292104,17.5050446643084,18.4739785199699));
#143182=CARTESIAN_POINT('Ctrl Pts',(16.7689574885197,17.5702050926227,18.4781935822529));
#143183=CARTESIAN_POINT('Ctrl Pts',(16.7151877112471,17.6346006473008,18.4823591668069));
#143184=CARTESIAN_POINT('Ctrl Pts',(16.6645463875622,17.701690347722,18.4865247513609));
#143185=CARTESIAN_POINT('Ctrl Pts',(16.6173078768048,17.7711338758054,18.4906903359149));
#143186=CARTESIAN_POINT('Ctrl Pts',(16.5700850499658,17.84055434756,18.4948545374302));
#143187=CARTESIAN_POINT('Ctrl Pts',(16.5262630517187,17.9123267137652,18.4990187389455));
#143188=CARTESIAN_POINT('Ctrl Pts',(16.4860739671285,17.9860801859963,18.5031829404608));
#143189=CARTESIAN_POINT('Ctrl Pts',(16.4458860826637,18.0598314558034,18.5073470176248));
#143190=CARTESIAN_POINT('Ctrl Pts',(16.4093311160891,18.1355633083681,18.5115110947889));
#143191=CARTESIAN_POINT('Ctrl Pts',(16.3765953977375,18.2128799965778,18.5156751719529));
#143192=CARTESIAN_POINT('Ctrl Pts',(16.3431614559388,18.2918457802489,18.5199280651398));
#143193=CARTESIAN_POINT('Ctrl Pts',(16.3137117771032,18.3724643312945,18.5241809583268));
#143194=CARTESIAN_POINT('Ctrl Pts',(16.2883925214927,18.4542939401133,18.5284338515138));
#143195=CARTESIAN_POINT('Ctrl Pts',(16.2635663208298,18.534530038676,18.5326039259141));
#143196=CARTESIAN_POINT('Ctrl Pts',(16.2427111716314,18.6159299801766,18.5367740003144));
#143197=CARTESIAN_POINT('Ctrl Pts',(16.2259135016088,18.6980651926532,18.5409440747148));
#143198=CARTESIAN_POINT('Ctrl Pts',(16.2086154222953,18.7826472458752,18.545238377295));
#143199=CARTESIAN_POINT('Ctrl Pts',(16.1956204803926,18.8680085473305,18.5495326798753));
#143200=CARTESIAN_POINT('Ctrl Pts',(16.1869656326132,18.9536754357807,18.5538269824556));
#143201=CARTESIAN_POINT('Ctrl Pts',(16.1783107848339,19.0393423242308,18.5581212850358));
#143202=CARTESIAN_POINT('Ctrl Pts',(16.1739959871027,19.125314270194,18.5624155876161));
#143203=CARTESIAN_POINT('Ctrl Pts',(16.1740000028035,19.2111198080496,18.5667098901964));
#143204=CARTESIAN_POINT('Ctrl Pts',(16.1740000028035,19.2111198086916,18.5667098902285));
#143205=CARTESIAN_POINT('Ctrl Pts',(16.1740003013853,19.2174997239769,18.5670291853155));
#143206=CARTESIAN_POINT('Ctrl Pts',(16.1740244495167,19.223879573923,18.5673484804024));
#143207=CARTESIAN_POINT('Ctrl Pts',(16.1740724460423,19.2302592442234,18.5676677754894));
#143208=CARTESIAN_POINT('Ctrl Pts',(16.1747014814392,19.31387026376,18.5718524098819));
#143209=CARTESIAN_POINT('Ctrl Pts',(16.1794322843349,19.3976060296583,18.5760370442745));
#143210=CARTESIAN_POINT('Ctrl Pts',(16.1882813814472,19.4810309522136,18.580221678667));
#143211=CARTESIAN_POINT('Ctrl Pts',(16.197117882965,19.5643371297178,18.5844003567505));
#143212=CARTESIAN_POINT('Ctrl Pts',(16.2100609870472,19.6473328891642,18.5885790348339));
#143213=CARTESIAN_POINT('Ctrl Pts',(16.2270752140173,19.7295827970784,18.5927577129174));
#143214=CARTESIAN_POINT('Ctrl Pts',(16.2443944087804,19.8133069754922,18.5970112908029));
#143215=CARTESIAN_POINT('Ctrl Pts',(16.2659321081158,19.8962578184692,18.6012648686885));
#143216=CARTESIAN_POINT('Ctrl Pts',(16.2915956147073,19.9779816286607,18.6055184465741));
#143217=CARTESIAN_POINT('Ctrl Pts',(16.3167615841416,20.058121063309,18.6096895605515));
#143218=CARTESIAN_POINT('Ctrl Pts',(16.3458946705845,20.1370801583406,18.613860674529));
#143219=CARTESIAN_POINT('Ctrl Pts',(16.3788563531112,20.2144432731945,18.6180317885065));
#143220=CARTESIAN_POINT('Ctrl Pts',(16.4118069750271,20.2917804281082,18.6222015028263));
#143221=CARTESIAN_POINT('Ctrl Pts',(16.4485834613786,20.3675222435802,18.6263712171462));
#143222=CARTESIAN_POINT('Ctrl Pts',(16.4889988104969,20.4412721890418,18.6305409314661));
#143223=CARTESIAN_POINT('Ctrl Pts',(16.5294127214636,20.5150195101638,18.6347104974097));
#143224=CARTESIAN_POINT('Ctrl Pts',(16.5734650159173,20.5867746991837,18.6388800633532));
#143225=CARTESIAN_POINT('Ctrl Pts',(16.620922959331,20.6561662258016,18.6430496292968));
#143226=CARTESIAN_POINT('Ctrl Pts',(16.6700494655017,20.7279974729095,18.6473657920363));
#143227=CARTESIAN_POINT('Ctrl Pts',(16.7228252639787,20.7972953169818,18.6516819547758));
#143228=CARTESIAN_POINT('Ctrl Pts',(16.7789448088305,20.8636824254772,18.6559981175153));
#143229=CARTESIAN_POINT('Ctrl Pts',(16.8332362653982,20.9279069808804,18.6601736817065));
#143230=CARTESIAN_POINT('Ctrl Pts',(16.8906566126945,20.9894072108734,18.6643492458977));
#143231=CARTESIAN_POINT('Ctrl Pts',(16.9508909514353,21.0478783631277,18.668524810089));
#143232=CARTESIAN_POINT('Ctrl Pts',(17.0141675834551,21.1093027543025,18.6729112721026));
#143233=CARTESIAN_POINT('Ctrl Pts',(17.0805495076474,21.1673836440658,18.6772977341163));
#143234=CARTESIAN_POINT('Ctrl Pts',(17.149633344248,21.2218163268039,18.6816841961299));
#143235=CARTESIAN_POINT('Ctrl Pts',(17.2187171808487,21.276249009542,18.6860706581435));
#143236=CARTESIAN_POINT('Ctrl Pts',(17.2905024122582,21.327033212256,18.6904571201572));
#143237=CARTESIAN_POINT('Ctrl Pts',(17.3645537444777,21.3739186191894,18.6948435821708));
#143238=CARTESIAN_POINT('Ctrl Pts',(17.435197865104,21.4186467590315,18.6990282165633));
#143239=CARTESIAN_POINT('Ctrl Pts',(17.5081670866297,21.4599934843659,18.7032128509557));
#143240=CARTESIAN_POINT('Ctrl Pts',(17.5831040926458,21.497709122393,18.7073974853482));
#143241=CARTESIAN_POINT('Ctrl Pts',(17.6579344351091,21.5353710768775,18.7115761634316));
#143242=CARTESIAN_POINT('Ctrl Pts',(17.7347265911909,21.5694120050826,18.7157548415149));
#143243=CARTESIAN_POINT('Ctrl Pts',(17.8130952257719,21.5996260479204,18.7199335195983));
#143244=CARTESIAN_POINT('Ctrl Pts',(17.8928685618191,21.630381655767,18.7241870974839));
#143245=CARTESIAN_POINT('Ctrl Pts',(17.9742750416619,21.6571715770569,18.7284406753695));
#143246=CARTESIAN_POINT('Ctrl Pts',(18.0568830023299,21.6798281777933,18.732694253255));
#143247=CARTESIAN_POINT('Ctrl Pts',(18.1378894464698,21.7020455361098,18.7368653672324));
#143248=CARTESIAN_POINT('Ctrl Pts',(18.2200507369794,21.7202882813848,18.7410364812097));
#143249=CARTESIAN_POINT('Ctrl Pts',(18.3029424071742,21.734447909442,18.7452075951871));
#143250=CARTESIAN_POINT('Ctrl Pts',(18.3858062622684,21.7486027860993,18.7493773095069));
#143251=CARTESIAN_POINT('Ctrl Pts',(18.469399557216,21.7586771892408,18.7535470238266));
#143252=CARTESIAN_POINT('Ctrl Pts',(18.5532876521045,21.7646137232005,18.7577167381464));
#143253=CARTESIAN_POINT('Ctrl Pts',(18.6371727618945,21.7705500459129,18.7618863040899));
#143254=CARTESIAN_POINT('Ctrl Pts',(18.7213521918226,21.7723487605766,18.7660558700333));
#143255=CARTESIAN_POINT('Ctrl Pts',(18.8053875689174,21.7700044577929,18.7702254359767));
#143256=CARTESIAN_POINT('Ctrl Pts',(18.8923775262288,21.7675777322146,18.7745415987164));
#143257=CARTESIAN_POINT('Ctrl Pts',(18.9792125852182,21.7607112463061,18.778857761456));
#143258=CARTESIAN_POINT('Ctrl Pts',(19.0654100827151,21.7494576728941,18.7831739241956));
#143259=CARTESIAN_POINT('Ctrl Pts',(19.1487997057715,21.7385706834556,18.7873494883867));
#143260=CARTESIAN_POINT('Ctrl Pts',(19.2315922114994,21.7235781663988,18.7915250525778));
#143261=CARTESIAN_POINT('Ctrl Pts',(19.3133609024084,21.7045799455322,18.7957006167688));
#143262=CARTESIAN_POINT('Ctrl Pts',(19.3992595355479,21.6846221696845,18.8000870787827));
#143263=CARTESIAN_POINT('Ctrl Pts',(19.4840276488775,21.6602435606427,18.8044735407967));
#143264=CARTESIAN_POINT('Ctrl Pts',(19.5671906913808,21.6316183655827,18.8088600028106));
#143265=CARTESIAN_POINT('Ctrl Pts',(19.6503537338841,21.6029931705227,18.8132464648245));
#143266=CARTESIAN_POINT('Ctrl Pts',(19.7319111958455,21.5701216768946,18.8176329268384));
#143267=CARTESIAN_POINT('Ctrl Pts',(19.8114169849415,21.5332344068934,18.8220193888523));
#143268=CARTESIAN_POINT('Ctrl Pts',(19.8872645948573,21.4980443748502,18.8262040232484));
#143269=CARTESIAN_POINT('Ctrl Pts',(19.9615275033059,21.4590690053604,18.8303886576445));
#143270=CARTESIAN_POINT('Ctrl Pts',(20.0338023663787,21.4164736018271,18.8345732920406));
#143271=CARTESIAN_POINT('Ctrl Pts',(20.10597435513,21.3739388275784,18.8387519701276));
#143272=CARTESIAN_POINT('Ctrl Pts',(20.1761635263181,21.3277944856882,18.8429306482147));
#143273=CARTESIAN_POINT('Ctrl Pts',(20.243988210436,21.2782531543921,18.8471093263017));
#143274=CARTESIAN_POINT('Ctrl Pts',(20.3130286032089,21.2278238303834,18.8513629041863));
#143275=CARTESIAN_POINT('Ctrl Pts',(20.3796184709323,21.1738747399783,18.855616482071));
#143276=CARTESIAN_POINT('Ctrl Pts',(20.443383208966,21.1166781063194,18.8598700599557));
#143277=CARTESIAN_POINT('Ctrl Pts',(20.5059117431835,21.0605903409627,18.8640411739367));
#143278=CARTESIAN_POINT('Ctrl Pts',(20.5657233532605,21.0013801499083,18.8682122879177));
#143279=CARTESIAN_POINT('Ctrl Pts',(20.6224970485899,20.9393457112126,18.8723834018987));
#143280=CARTESIAN_POINT('Ctrl Pts',(20.6792516929575,20.8773320887721,18.8765531162222));
#143281=CARTESIAN_POINT('Ctrl Pts',(20.7329701367994,20.8124964399258,18.8807228305456));
#143282=CARTESIAN_POINT('Ctrl Pts',(20.7833688571021,20.745173160872,18.884892544869));
#143283=CARTESIAN_POINT('Ctrl Pts',(20.833765784002,20.6778522774696,18.8890621108161));
#143284=CARTESIAN_POINT('Ctrl Pts',(20.8808429472262,20.6080443086443,18.8932316767632));
#143285=CARTESIAN_POINT('Ctrl Pts',(20.9243585153512,20.5361149286867,18.8974012427103));
#143286=CARTESIAN_POINT('Ctrl Pts',(20.9694040370983,20.4616566005815,18.9017174054456));
#143287=CARTESIAN_POINT('Ctrl Pts',(21.0106325794989,20.3849253593978,18.9060335681809));
#143288=CARTESIAN_POINT('Ctrl Pts',(21.0478271756457,20.306355559279,18.9103497309162));
#143289=CARTESIAN_POINT('Ctrl Pts',(21.0838101617912,20.2303451620166,18.9145252951108));
#143290=CARTESIAN_POINT('Ctrl Pts',(21.1160178406327,20.1526146016966,18.9187008593055));
#143291=CARTESIAN_POINT('Ctrl Pts',(21.1443031849367,20.0735766961168,18.9228764235001));
#143292=CARTESIAN_POINT('Ctrl Pts',(21.1740171546712,19.9905467740118,18.9272628855057));
#143293=CARTESIAN_POINT('Ctrl Pts',(21.1994019743872,19.9060745270037,18.9316493475113));
#143294=CARTESIAN_POINT('Ctrl Pts',(21.2203472929199,19.8206532940858,18.9360358095169));
#143295=CARTESIAN_POINT('Ctrl Pts',(21.2412926114527,19.735232061168,18.9404222715225));
#143296=CARTESIAN_POINT('Ctrl Pts',(21.257798394603,19.6488624265219,18.9448087335281));
#143297=CARTESIAN_POINT('Ctrl Pts',(21.2698170137415,19.5620442604844,18.9491951955337));
#143298=CARTESIAN_POINT('Ctrl Pts',(21.2812826384042,19.4792207269144,18.9533798299225));
#143299=CARTESIAN_POINT('Ctrl Pts',(21.2887076244829,19.3956807451278,18.9575644643113));
#143300=CARTESIAN_POINT('Ctrl Pts',(21.2920126435715,19.3118529391169,18.9617490987001));
#143301=CARTESIAN_POINT('Ctrl Pts',(21.2953129583745,19.228144451612,18.9659277767799));
#143302=CARTESIAN_POINT('Ctrl Pts',(21.294504936491,19.1441494093845,18.9701064548596));
#143303=CARTESIAN_POINT('Ctrl Pts',(21.2895607321101,19.0603038006549,18.9742851329393));
#143304=CARTESIAN_POINT('Ctrl Pts',(21.2845279064127,18.9749553195403,18.9785387108258));
#143305=CARTESIAN_POINT('Ctrl Pts',(21.2752090914542,18.8897621593927,18.9827922887123));
#143306=CARTESIAN_POINT('Ctrl Pts',(21.2616304174303,18.8051866526579,18.9870458665988));
#143307=CARTESIAN_POINT('Ctrl Pts',(21.2483149925156,18.7222508072601,18.9912169805726));
#143308=CARTESIAN_POINT('Ctrl Pts',(21.2309034822292,18.6399093552897,18.9953880945464));
#143309=CARTESIAN_POINT('Ctrl Pts',(21.2094728610011,18.5585935971749,18.9995592085202));
#143310=CARTESIAN_POINT('Ctrl Pts',(21.1880494310247,18.4773051253474,19.0037289228364));
#143311=CARTESIAN_POINT('Ctrl Pts',(21.1626096856898,18.3970421082987,19.0078986371526));
#143312=CARTESIAN_POINT('Ctrl Pts',(21.1332813336496,18.3182239463334,19.0120683514689));
#143313=CARTESIAN_POINT('Ctrl Pts',(21.1039540252378,18.2394085890558,19.0162379174088));
#143314=CARTESIAN_POINT('Ctrl Pts',(21.0707385464732,18.1620384154915,19.0204074833488));
#143315=CARTESIAN_POINT('Ctrl Pts',(21.0338114728017,18.0865147001541,19.0245770492887));
#143316=CARTESIAN_POINT('Ctrl Pts',(20.9955860886931,18.0083356639876,19.0288932120326));
#143317=CARTESIAN_POINT('Ctrl Pts',(20.9533834858384,17.9321358186686,19.0332093747765));
#143318=CARTESIAN_POINT('Ctrl Pts',(20.9074514472649,17.8583327066931,19.0375255375203));
#143319=CARTESIAN_POINT('Ctrl Pts',(20.8630156401098,17.7869337234772,19.041701101708));
#143320=CARTESIAN_POINT('Ctrl Pts',(20.8150899458169,17.7177780846045,19.0458766658958));
#143321=CARTESIAN_POINT('Ctrl Pts',(20.7639418957711,17.6512128671536,19.0500522300835));
#143322=CARTESIAN_POINT('Ctrl Pts',(20.7102104791443,17.5812855985968,19.0544386921054));
#143323=CARTESIAN_POINT('Ctrl Pts',(20.6529230087042,17.5142177570107,19.0588251541274));
#143324=CARTESIAN_POINT('Ctrl Pts',(20.5924345734847,17.4503691653055,19.0632116161493));
#143325=CARTESIAN_POINT('Ctrl Pts',(20.5319461382652,17.3865205736004,19.0675980781713));
#143326=CARTESIAN_POINT('Ctrl Pts',(20.468257210959,17.3258915767387,19.0719845401932));
#143327=CARTESIAN_POINT('Ctrl Pts',(20.4017623229458,17.2687927931958,19.0763710022152));
#143328=CARTESIAN_POINT('Ctrl Pts',(20.3665290189526,17.2385381547066,19.0786952342651));
#143329=CARTESIAN_POINT('Ctrl Pts',(20.3304358403751,17.2092113636734,19.0810194663149));
#143330=CARTESIAN_POINT('Ctrl Pts',(20.2935357313021,17.1808649545431,19.0833436983648));
#143331=CARTESIAN_POINT('Origin',(18.734,19.211,-1.76670989022852));
#143332=CARTESIAN_POINT('',(20.2935357313021,17.1808649545432,19.9498236335591));
#143333=CARTESIAN_POINT('',(20.2935357313021,17.1808649545432,19.8833624920292));
#143334=CARTESIAN_POINT('',(20.2935357313021,17.1808649545432,-1.76670989022852));
#143335=CARTESIAN_POINT('',(16.1740009418753,19.2131959965388,19.4332901097715));
#143336=CARTESIAN_POINT('Ctrl Pts',(16.1740009418753,19.2131959965388,19.4332901097715));
#143337=CARTESIAN_POINT('Ctrl Pts',(16.1741094126172,19.3396465587508,19.4395926510338));
#143338=CARTESIAN_POINT('Ctrl Pts',(16.1835900621655,19.4657089276735,19.4458951922961));
#143339=CARTESIAN_POINT('Ctrl Pts',(16.2022529884087,19.5902849447293,19.4521977335585));
#143340=CARTESIAN_POINT('Ctrl Pts',(16.2064836512067,19.6185248420538,19.4536264444961));
#143341=CARTESIAN_POINT('Ctrl Pts',(16.2111860003675,19.6466884926971,19.4550551554337));
#143342=CARTESIAN_POINT('Ctrl Pts',(16.2163575306344,19.6747632978648,19.4564838663713));
#143343=CARTESIAN_POINT('Ctrl Pts',(16.2315047248246,19.7569932189491,19.4606685004926));
#143344=CARTESIAN_POINT('Ctrl Pts',(16.2507129697403,19.838633291604,19.4648531346138));
#143345=CARTESIAN_POINT('Ctrl Pts',(16.273922855402,19.9192516802849,19.4690377687351));
#143346=CARTESIAN_POINT('Ctrl Pts',(16.2970997046635,19.9997553186653,19.4732164465475));
#143347=CARTESIAN_POINT('Ctrl Pts',(16.3242667547551,20.0792397233557,19.4773951243598));
#143348=CARTESIAN_POINT('Ctrl Pts',(16.3553134075107,20.1572822489679,19.4815738021722));
#143349=CARTESIAN_POINT('Ctrl Pts',(16.3869165517625,20.2367236371946,19.4858273801256));
#143350=CARTESIAN_POINT('Ctrl Pts',(16.4225396637635,20.31467047214,19.4900809580789));
#143351=CARTESIAN_POINT('Ctrl Pts',(16.4620126245789,20.3906920640265,19.4943345360323));
#143352=CARTESIAN_POINT('Ctrl Pts',(16.500720321909,20.4652398230115,19.4985056497412));
#143353=CARTESIAN_POINT('Ctrl Pts',(16.543129704132,20.537935895187,19.5026767634501));
#143354=CARTESIAN_POINT('Ctrl Pts',(16.5890321382678,20.6083950308112,19.506847877159));
#143355=CARTESIAN_POINT('Ctrl Pts',(16.6349191694141,20.678830523216,19.5110175912119));
#143356=CARTESIAN_POINT('Ctrl Pts',(16.6842966737088,20.7470301846918,19.5151873052647));
#143357=CARTESIAN_POINT('Ctrl Pts',(16.7369115952943,20.8126360085207,19.5193570193175));
#143358=CARTESIAN_POINT('Ctrl Pts',(16.7895246446383,20.8782394978417,19.5235265849959));
#143359=CARTESIAN_POINT('Ctrl Pts',(16.845374593747,20.9412489746849,19.5276961506742));
#143360=CARTESIAN_POINT('Ctrl Pts',(16.9041676934323,21.0013389985813,19.5318657163526));
#143361=CARTESIAN_POINT('Ctrl Pts',(16.9650278943555,21.0635417221558,19.5361818794109));
#143362=CARTESIAN_POINT('Ctrl Pts',(17.0290416909492,21.1226154992726,19.5404980424693));
#143363=CARTESIAN_POINT('Ctrl Pts',(17.0958426218354,21.1782418266103,19.5448142055276));
#143364=CARTESIAN_POINT('Ctrl Pts',(17.1604675106422,21.2320561248729,19.5489897694609));
#143365=CARTESIAN_POINT('Ctrl Pts',(17.2277003349656,21.2826438809482,19.5531653333942));
#143366=CARTESIAN_POINT('Ctrl Pts',(17.2971780335787,21.3297596930302,19.5573408973275));
#143367=CARTESIAN_POINT('Ctrl Pts',(17.3701649002202,21.3792552227006,19.5617273599483));
#143368=CARTESIAN_POINT('Ctrl Pts',(17.4456288796132,21.4249185512742,19.5661138225692));
#143369=CARTESIAN_POINT('Ctrl Pts',(17.5231197837688,21.466519696642,19.5705002851901));
#143370=CARTESIAN_POINT('Ctrl Pts',(17.6006106879243,21.5081208420097,19.574886747811));
#143371=CARTESIAN_POINT('Ctrl Pts',(17.6801279596808,21.54565962526,19.5792732104319));
#143372=CARTESIAN_POINT('Ctrl Pts',(17.7611994326903,21.5789651720923,19.5836596730527));
#143373=CARTESIAN_POINT('Ctrl Pts',(17.8385406770856,21.6107382772506,19.587844307487));
#143374=CARTESIAN_POINT('Ctrl Pts',(17.9175841221713,21.6387774071546,19.5920289419213));
#143375=CARTESIAN_POINT('Ctrl Pts',(17.9979345050497,21.6628987717978,19.5962135763555));
#143376=CARTESIAN_POINT('Ctrl Pts',(18.0781705190567,21.6869858026501,19.6003922544782));
#143377=CARTESIAN_POINT('Ctrl Pts',(18.1597093389463,21.7071660136985,19.6045709326009));
#143378=CARTESIAN_POINT('Ctrl Pts',(18.2421357220941,21.723303630559,19.6087496107235));
#143379=CARTESIAN_POINT('Ctrl Pts',(18.3260395379464,21.7397305024131,19.613003188599));
#143380=CARTESIAN_POINT('Ctrl Pts',(18.4108626031778,21.751968244467,19.6172567664744));
#143381=CARTESIAN_POINT('Ctrl Pts',(18.4961506937664,21.7599267756301,19.6215103443499));
#143382=CARTESIAN_POINT('Ctrl Pts',(18.5797853091396,21.7677310152159,19.6256814583602));
#143383=CARTESIAN_POINT('Ctrl Pts',(18.6638666007977,21.7714204401678,19.6298525723706));
#143384=CARTESIAN_POINT('Ctrl Pts',(18.7479577055539,21.7709619494156,19.634023686381));
#143385=CARTESIAN_POINT('Ctrl Pts',(18.8320205926795,21.7705036125146,19.6381934007314));
#143386=CARTESIAN_POINT('Ctrl Pts',(18.9160928267202,21.7659001267025,19.6423631150818));
#143387=CARTESIAN_POINT('Ctrl Pts',(18.9997364062976,21.7571704896507,19.6465328294322));
#143388=CARTESIAN_POINT('Ctrl Pts',(19.0833770094289,21.7484411632419,19.6507023954039));
#143389=CARTESIAN_POINT('Ctrl Pts',(19.1665885309657,21.7355860261267,19.6548719613755));
#143390=CARTESIAN_POINT('Ctrl Pts',(19.2489383260605,21.7186759201209,19.6590415273471));
#143391=CARTESIAN_POINT('Ctrl Pts',(19.334183437007,21.7011712759268,19.6633576900461));
#143392=CARTESIAN_POINT('Ctrl Pts',(19.4185045808363,21.6793213182574,19.667673852745));
#143393=CARTESIAN_POINT('Ctrl Pts',(19.501435588217,21.653261783253,19.6719900154439));
#143394=CARTESIAN_POINT('Ctrl Pts',(19.581665127909,21.6280511344977,19.6761655796569));
#143395=CARTESIAN_POINT('Ctrl Pts',(19.6605932821677,21.5989011580776,19.68034114387));
#143396=CARTESIAN_POINT('Ctrl Pts',(19.737817188692,21.5659842996688,19.684516708083));
#143397=CARTESIAN_POINT('Ctrl Pts',(19.8189414894304,21.5314048897282,19.6889031700249));
#143398=CARTESIAN_POINT('Ctrl Pts',(19.8981843303167,21.4926683234582,19.6932896319667));
#143399=CARTESIAN_POINT('Ctrl Pts',(19.9751086547793,21.4500286525705,19.6976760939086));
#143400=CARTESIAN_POINT('Ctrl Pts',(20.052032979242,21.4073889816829,19.7020625558505));
#143401=CARTESIAN_POINT('Ctrl Pts',(20.1266383352643,21.3608465778203,19.7064490177923));
#143402=CARTESIAN_POINT('Ctrl Pts',(20.1985254700751,21.3107059669157,19.7108354797342));
#143403=CARTESIAN_POINT('Ctrl Pts',(20.2671049874815,21.2628723885244,19.7150201150502));
#143404=CARTESIAN_POINT('Ctrl Pts',(20.333466190131,21.2115863975067,19.7192047503662));
#143405=CARTESIAN_POINT('Ctrl Pts',(20.397240591338,21.1570808655669,19.7233893856822));
#143406=CARTESIAN_POINT('Ctrl Pts',(20.4609242176641,21.1026529154322,19.7275680646934));
#143407=CARTESIAN_POINT('Ctrl Pts',(20.5220280094148,21.0450148232166,19.7317467437045));
#143408=CARTESIAN_POINT('Ctrl Pts',(20.5802130388127,20.9844422503476,19.7359254227157));
#143409=CARTESIAN_POINT('Ctrl Pts',(20.6394409766828,20.922783974677,19.7401790003699));
#143410=CARTESIAN_POINT('Ctrl Pts',(20.6956440915829,20.8580852599725,19.7444325780241));
#143411=CARTESIAN_POINT('Ctrl Pts',(20.748500776934,20.7906792774903,19.7486861556782));
#143412=CARTESIAN_POINT('Ctrl Pts',(20.8003327466861,20.7245800731623,19.7528572705872));
#143413=CARTESIAN_POINT('Ctrl Pts',(20.8489465843895,20.655878012879,19.7570283854962));
#143414=CARTESIAN_POINT('Ctrl Pts',(20.8940779914836,20.5849225126288,19.7611995004052));
#143415=CARTESIAN_POINT('Ctrl Pts',(20.939194254295,20.5139908221869,19.7653692156561));
#143416=CARTESIAN_POINT('Ctrl Pts',(20.9808301605939,20.4408075813748,19.7695389309069));
#143417=CARTESIAN_POINT('Ctrl Pts',(21.0187646025393,20.3657513632741,19.7737086461577));
#143418=CARTESIAN_POINT('Ctrl Pts',(21.0566976945983,20.2906978160278,19.7778782130304));
#143419=CARTESIAN_POINT('Ctrl Pts',(21.0909293774397,20.2137718349661,19.7820477799031));
#143420=CARTESIAN_POINT('Ctrl Pts',(21.1212850353342,20.1353755514236,19.7862173467758));
#143421=CARTESIAN_POINT('Ctrl Pts',(21.1527079456892,20.0542229900628,19.7905335084124));
#143422=CARTESIAN_POINT('Ctrl Pts',(21.1799770112795,19.9714953041982,19.7948496700491));
#143423=CARTESIAN_POINT('Ctrl Pts',(21.2029540362409,19.887657939383,19.7991658316857));
#143424=CARTESIAN_POINT('Ctrl Pts',(21.2251825975767,19.8065515294293,19.8033413967921));
#143425=CARTESIAN_POINT('Ctrl Pts',(21.2433943908868,19.7244070949879,19.8075169618984));
#143426=CARTESIAN_POINT('Ctrl Pts',(21.257516353913,19.6416567212221,19.8116925270047));
#143427=CARTESIAN_POINT('Ctrl Pts',(21.2723515733316,19.5547268836692,19.8160789869065));
#143428=CARTESIAN_POINT('Ctrl Pts',(21.2826728879128,19.4671288669274,19.8204654468084));
#143429=CARTESIAN_POINT('Ctrl Pts',(21.2884573444648,19.3793676789345,19.8248519067102));
#143430=CARTESIAN_POINT('Ctrl Pts',(21.2942418010168,19.2916064909416,19.829238366612));
#143431=CARTESIAN_POINT('Ctrl Pts',(21.2954894673636,19.2036827129334,19.8336248265138));
#143432=CARTESIAN_POINT('Ctrl Pts',(21.2922402934572,19.1160968866051,19.8380112864157));
#143433=CARTESIAN_POINT('Ctrl Pts',(21.2891403572396,19.0325339616877,19.8421962719869));
#143434=CARTESIAN_POINT('Ctrl Pts',(21.281936068755,18.9489675609148,19.8463812575582));
#143435=CARTESIAN_POINT('Ctrl Pts',(21.27062378234,18.865833682311,19.8505662431294));
#143436=CARTESIAN_POINT('Ctrl Pts',(21.2593308428941,18.7828419843874,19.8547440712805));
#143437=CARTESIAN_POINT('Ctrl Pts',(21.2439439373047,18.7002817896674,19.8589218994317));
#143438=CARTESIAN_POINT('Ctrl Pts',(21.2245113674061,18.6185870284835,19.8630997275828));
#143439=CARTESIAN_POINT('Ctrl Pts',(21.205097707692,18.5369717659459,19.867273490214));
#143440=CARTESIAN_POINT('Ctrl Pts',(21.1816463054595,18.4562207098548,19.8714472528451));
#143441=CARTESIAN_POINT('Ctrl Pts',(21.1542568723911,18.3767598237656,19.8756210154763));
#143442=CARTESIAN_POINT('Ctrl Pts',(21.1268858754456,18.2973524236562,19.8797919687028));
#143443=CARTESIAN_POINT('Ctrl Pts',(21.0955822614867,18.219233902462,19.8839629219293));
#143444=CARTESIAN_POINT('Ctrl Pts',(21.0604958059402,18.1428159030661,19.8881338751558));
#143445=CARTESIAN_POINT('Ctrl Pts',(21.0254224420134,18.0664264171056,19.8923032720971));
#143446=CARTESIAN_POINT('Ctrl Pts',(20.9865692332511,17.9917366095586,19.8964726690383));
#143447=CARTESIAN_POINT('Ctrl Pts',(20.9441338701527,17.9191376714201,19.9006420659796));
#143448=CARTESIAN_POINT('Ctrl Pts',(20.9016818644379,17.84651026089,19.904813098106));
#143449=CARTESIAN_POINT('Ctrl Pts',(20.8556451221797,17.7759757602288,19.9089841302323));
#143450=CARTESIAN_POINT('Ctrl Pts',(20.8062666824223,17.7078996051752,19.9131551623587));
#143451=CARTESIAN_POINT('Ctrl Pts',(20.756880639062,17.6398129673268,19.9173268367668));
#143452=CARTESIAN_POINT('Ctrl Pts',(20.7041521537383,17.5741857944587,19.921498511175));
#143453=CARTESIAN_POINT('Ctrl Pts',(20.6483656429806,17.5113517466913,19.9256701855831));
#143454=CARTESIAN_POINT('Ctrl Pts',(20.5925104930342,17.448440388513,19.9298469927795));
#143455=CARTESIAN_POINT('Ctrl Pts',(20.5335901157611,17.3883293580182,19.9340237999759));
#143456=CARTESIAN_POINT('Ctrl Pts',(20.4719267477955,17.3313163512716,19.9382006071723));
#143457=CARTESIAN_POINT('Ctrl Pts',(20.4147287558635,17.278431962898,19.9420749493012));
#143458=CARTESIAN_POINT('Ctrl Pts',(20.3551712638459,17.2282129452766,19.9459492914302));
#143459=CARTESIAN_POINT('Ctrl Pts',(20.2935357313021,17.1808649545432,19.9498236335591));
#143460=CARTESIAN_POINT('Ctrl Pts',(20.2912840337091,17.1837659559064,19.1498287221711));
#143461=CARTESIAN_POINT('Ctrl Pts',(20.0133685819973,16.9682014306898,19.1672632324502));
#143462=CARTESIAN_POINT('Ctrl Pts',(18.916759280455,16.4174581264604,19.2270896782898));
#143463=CARTESIAN_POINT('Ctrl Pts',(16.8320816456072,16.9602242617438,19.3215765971066));
#143464=CARTESIAN_POINT('Ctrl Pts',(16.1790132394519,18.5174132428891,19.3986290056444));
#143465=CARTESIAN_POINT('Ctrl Pts',(16.1726852608311,19.213184455598,19.4332894786216));
#143466=CARTESIAN_POINT('',(16.1740010149448,19.2087204131752,19.3667098901939));
#143467=CARTESIAN_POINT('Ctrl Pts',(20.2935357313021,17.1808649545431,19.0833436983648));
#143468=CARTESIAN_POINT('Ctrl Pts',(20.227154634791,17.1298714543207,19.0875248532691));
#143469=CARTESIAN_POINT('Ctrl Pts',(20.1581601772516,17.082052917846,19.0917060081733));
#143470=CARTESIAN_POINT('Ctrl Pts',(20.0868893350051,17.0376867581433,19.0958871630776));
#143471=CARTESIAN_POINT('Ctrl Pts',(20.0157068252627,16.9933755854993,19.1000631358923));
#143472=CARTESIAN_POINT('Ctrl Pts',(19.9422539237334,16.9525085306642,19.1042391087071));
#143473=CARTESIAN_POINT('Ctrl Pts',(19.8668988922355,16.9153214292999,19.1084150815218));
#143474=CARTESIAN_POINT('Ctrl Pts',(19.7916121501407,16.8781680282063,19.1125872699219));
#143475=CARTESIAN_POINT('Ctrl Pts',(19.7144271146915,16.8446881560225,19.1167594583219));
#143476=CARTESIAN_POINT('Ctrl Pts',(19.6357379644307,16.8150724878444,19.1209316467219));
#143477=CARTESIAN_POINT('Ctrl Pts',(19.5570861679343,16.7854708782332,19.1251018545828));
#143478=CARTESIAN_POINT('Ctrl Pts',(19.4769321042154,16.7597299921337,19.1292720624437));
#143479=CARTESIAN_POINT('Ctrl Pts',(19.3956902142815,16.7379925070222,19.1334422703046));
#143480=CARTESIAN_POINT('Ctrl Pts',(19.3144625191379,16.7162588199397,19.1376117495361));
#143481=CARTESIAN_POINT('Ctrl Pts',(19.232147819739,16.6985272628336,19.1417812287676));
#143482=CARTESIAN_POINT('Ctrl Pts',(19.1491746923774,16.6848903478255,19.1459507079991));
#143483=CARTESIAN_POINT('Ctrl Pts',(19.0661911726319,16.6712517247938,19.1501207094579));
#143484=CARTESIAN_POINT('Ctrl Pts',(18.9825495153131,16.6617088355055,19.1542907109167));
#143485=CARTESIAN_POINT('Ctrl Pts',(18.8986860774795,16.6563026606104,19.1584607123754));
#143486=CARTESIAN_POINT('Ctrl Pts',(18.8147324189666,16.650890669727,19.1626351999413));
#143487=CARTESIAN_POINT('Ctrl Pts',(18.7305569635541,16.6496243068978,19.1668096875072));
#143488=CARTESIAN_POINT('Ctrl Pts',(18.6465982265326,16.6524924408955,19.1709841750731));
#143489=CARTESIAN_POINT('Ctrl Pts',(18.5625903672273,16.6553622529711,19.1751611050336));
#143490=CARTESIAN_POINT('Ctrl Pts',(18.4787999371148,16.6623713392017,19.179338034994));
#143491=CARTESIAN_POINT('Ctrl Pts',(18.3956600675484,16.6734566821217,19.1835149649545));
#143492=CARTESIAN_POINT('Ctrl Pts',(18.3123797908189,16.6845607460424,19.1876989489419));
#143493=CARTESIAN_POINT('Ctrl Pts',(18.2297527206121,16.6997547284267,19.1918829329294));
#143494=CARTESIAN_POINT('Ctrl Pts',(18.1482012114888,16.7189246039939,19.1960669169169));
#143495=CARTESIAN_POINT('Ctrl Pts',(18.0996034729978,16.7303482135597,19.1985602142434));
#143496=CARTESIAN_POINT('Ctrl Pts',(18.0513874007896,16.7431827575916,19.20105351157));
#143497=CARTESIAN_POINT('Ctrl Pts',(18.0036392138284,16.7573958913421,19.2035468088965));
#143498=CARTESIAN_POINT('Ctrl Pts',(17.9235008748349,16.7812505547995,19.2077314433106));
#143499=CARTESIAN_POINT('Ctrl Pts',(17.8443833236132,16.8090798944622,19.2119160777247));
#143500=CARTESIAN_POINT('Ctrl Pts',(17.7667095652053,16.8407786570123,19.2161007121388));
#143501=CARTESIAN_POINT('Ctrl Pts',(17.6891463657766,16.8724323002981,19.2202793902438));
#143502=CARTESIAN_POINT('Ctrl Pts',(17.6130232994518,16.9079442542207,19.2244580683488));
#143503=CARTESIAN_POINT('Ctrl Pts',(17.5387487593373,16.9471593537322,19.2286367464538));
#143504=CARTESIAN_POINT('Ctrl Pts',(17.4631429019463,16.9870773554683,19.232890324334));
#143505=CARTESIAN_POINT('Ctrl Pts',(17.3894529543325,17.0308324287606,19.2371439022142));
#143506=CARTESIAN_POINT('Ctrl Pts',(17.3180889421074,17.0782093688931,19.2413974800944));
#143507=CARTESIAN_POINT('Ctrl Pts',(17.2481084600744,17.1246678148849,19.2455685940934));
#143508=CARTESIAN_POINT('Ctrl Pts',(17.1803649335802,17.1746086808986,19.2497397080924));
#143509=CARTESIAN_POINT('Ctrl Pts',(17.1152190899139,17.2277833287458,19.2539108220915));
#143510=CARTESIAN_POINT('Ctrl Pts',(17.0500951065651,17.2809401333258,19.2580805364329));
#143511=CARTESIAN_POINT('Ctrl Pts',(16.9875674309667,17.337328274007,19.2622502507743));
#143512=CARTESIAN_POINT('Ctrl Pts',(16.9279649526866,17.3966578580996,19.2664199651157));
#143513=CARTESIAN_POINT('Ctrl Pts',(16.8683645953195,17.45598533099,19.2705895310807));
#143514=CARTESIAN_POINT('Ctrl Pts',(16.8116895537474,17.5182537140333,19.2747590970458));
#143515=CARTESIAN_POINT('Ctrl Pts',(16.7582319859915,17.5831361375039,19.2789286630108));
#143516=CARTESIAN_POINT('Ctrl Pts',(16.702894916699,17.6502997462159,19.2832448257247));
#143517=CARTESIAN_POINT('Ctrl Pts',(16.6510061189344,17.7202642276924,19.2875609884387));
#143518=CARTESIAN_POINT('Ctrl Pts',(16.6028430768051,17.7926311591414,19.2918771511526));
#143519=CARTESIAN_POINT('Ctrl Pts',(16.556248940208,17.8626407461605,19.2960527153649));
#143520=CARTESIAN_POINT('Ctrl Pts',(16.5131417547257,17.9348982385108,19.3002282795771));
#143521=CARTESIAN_POINT('Ctrl Pts',(16.4737266859811,18.0090164119531,19.3044038437894));
#143522=CARTESIAN_POINT('Ctrl Pts',(16.4323208564697,18.086878116905,19.3087903057542));
#143523=CARTESIAN_POINT('Ctrl Pts',(16.3949901703488,18.1667928797147,19.3131767677189));
#143524=CARTESIAN_POINT('Ctrl Pts',(16.3619151438302,18.2482884984951,19.3175632296837));
#143525=CARTESIAN_POINT('Ctrl Pts',(16.3288401173116,18.3297841172754,19.3219496916485));
#143526=CARTESIAN_POINT('Ctrl Pts',(16.3000208686933,18.4128600189268,19.3263361536133));
#143527=CARTESIAN_POINT('Ctrl Pts',(16.2755767948946,18.4970284707363,19.330722615578));
#143528=CARTESIAN_POINT('Ctrl Pts',(16.2465257453506,18.5970601546401,19.3359357942368));
#143529=CARTESIAN_POINT('Ctrl Pts',(16.2235642356451,18.6989346521906,19.3411489728956));
#143530=CARTESIAN_POINT('Ctrl Pts',(16.2068848499389,18.8019901977558,19.3463621515544));
#143531=CARTESIAN_POINT('Ctrl Pts',(16.1904712789818,18.9034033756426,19.3514922492292));
#143532=CARTESIAN_POINT('Ctrl Pts',(16.1801412136981,19.0059603454969,19.356622346904));
#143533=CARTESIAN_POINT('Ctrl Pts',(16.1760324691886,19.1090092586819,19.3617524445787));
#143534=CARTESIAN_POINT('Ctrl Pts',(16.1747089805831,19.1422028685768,19.3634049264505));
#143535=CARTESIAN_POINT('Ctrl Pts',(16.1740306434087,19.1754473495068,19.3650574083222));
#143536=CARTESIAN_POINT('Ctrl Pts',(16.1740010149447,19.2087204131752,19.3667098901939));
#143537=CARTESIAN_POINT('Ctrl Pts',(16.1740010149441,19.2087204138715,19.3667098902285));
#143538=CARTESIAN_POINT('Ctrl Pts',(16.173926819566,19.2920425969752,19.3708480242598));
#143539=CARTESIAN_POINT('Ctrl Pts',(16.1779248169782,19.3754486069208,19.374986158291));
#143540=CARTESIAN_POINT('Ctrl Pts',(16.1859928190663,19.4585063754938,19.3791242923223));
#143541=CARTESIAN_POINT('Ctrl Pts',(16.1940571655297,19.5415265104593,19.3832605513584));
#143542=CARTESIAN_POINT('Ctrl Pts',(16.2061878113245,19.6241982519121,19.3873968103945));
#143543=CARTESIAN_POINT('Ctrl Pts',(16.2223305526748,19.7060925038549,19.3915330694306));
#143544=CARTESIAN_POINT('Ctrl Pts',(16.2384710163523,19.7879752008633,19.395668744858));
#143545=CARTESIAN_POINT('Ctrl Pts',(16.2586223602412,19.8690801670325,19.3998044202854));
#143546=CARTESIAN_POINT('Ctrl Pts',(16.2826791433891,19.9489878440355,19.4039400957128));
#143547=CARTESIAN_POINT('Ctrl Pts',(16.3067400382207,20.0289091785212,19.4080764779923));
#143548=CARTESIAN_POINT('Ctrl Pts',(16.3347075604893,20.1076323699276,19.4122128602718));
#143549=CARTESIAN_POINT('Ctrl Pts',(16.3664266589092,20.1847538059263,19.4163492425514));
#143550=CARTESIAN_POINT('Ctrl Pts',(16.3981808282506,20.2619605129437,19.4204901983133));
#143551=CARTESIAN_POINT('Ctrl Pts',(16.4336946710478,20.3375614976538,19.4246311540753));
#143552=CARTESIAN_POINT('Ctrl Pts',(16.4727655806453,20.4111745292772,19.4287721098372));
#143553=CARTESIAN_POINT('Ctrl Pts',(16.5118617772824,20.4848352039083,19.4329157456625));
#143554=CARTESIAN_POINT('Ctrl Pts',(16.5545193804039,20.556504964772,19.4370593814878));
#143555=CARTESIAN_POINT('Ctrl Pts',(16.6004918491551,20.6258296612236,19.4412030173131));
#143556=CARTESIAN_POINT('Ctrl Pts',(16.6465392454204,20.6952673454551,19.4453534065789));
#143557=CARTESIAN_POINT('Ctrl Pts',(16.6959120078414,20.7623519651714,19.4495037958447));
#143558=CARTESIAN_POINT('Ctrl Pts',(16.7483230702952,20.826762089801,19.4536541851104));
#143559=CARTESIAN_POINT('Ctrl Pts',(16.7661884610687,20.848717608205,19.4550689308268));
#143560=CARTESIAN_POINT('Ctrl Pts',(16.7844065661404,20.8703626874017,19.4564836765431));
#143561=CARTESIAN_POINT('Ctrl Pts',(16.8029650799464,20.891685615317,19.4578984222595));
#143562=CARTESIAN_POINT('Ctrl Pts',(16.8578587574058,20.9547560712656,19.4620830566462));
#143563=CARTESIAN_POINT('Ctrl Pts',(16.915947800584,21.0152517076035,19.466267691033));
#143564=CARTESIAN_POINT('Ctrl Pts',(16.9769612646036,21.0728310563305,19.4704523254198));
#143565=CARTESIAN_POINT('Ctrl Pts',(17.0378878835037,21.1303284479763,19.4746310034971));
#143566=CARTESIAN_POINT('Ctrl Pts',(17.1017303233983,21.1849174841133,19.4788096815744));
#143567=CARTESIAN_POINT('Ctrl Pts',(17.1681782563646,21.2362906623887,19.4829883596517));
#143568=CARTESIAN_POINT('Ctrl Pts',(17.2358172209073,21.2885846680663,19.4872419375387));
#143569=CARTESIAN_POINT('Ctrl Pts',(17.306155687672,21.3375460297098,19.4914955154258));
#143570=CARTESIAN_POINT('Ctrl Pts',(17.3788280009098,21.382890617154,19.4957490933129));
#143571=CARTESIAN_POINT('Ctrl Pts',(17.4500914193923,21.4273561111915,19.4999202072833));
#143572=CARTESIAN_POINT('Ctrl Pts',(17.5235985912763,21.46834356131,19.5040913212538));
#143573=CARTESIAN_POINT('Ctrl Pts',(17.5989738385243,21.5056275542592,19.5082624352243));
#143574=CARTESIAN_POINT('Ctrl Pts',(17.6743237928747,21.5428990362019,19.5124321495369));
#143575=CARTESIAN_POINT('Ctrl Pts',(17.7515401656511,21.5764693252641,19.5166018638495));
#143576=CARTESIAN_POINT('Ctrl Pts',(17.8302229081156,21.6061590694952,19.5207715781621));
#143577=CARTESIAN_POINT('Ctrl Pts',(17.9089028507052,21.6358477572358,19.5249411440981));
#143578=CARTESIAN_POINT('Ctrl Pts',(17.9890486285244,21.6616560130853,19.5291107100341));
#143579=CARTESIAN_POINT('Ctrl Pts',(18.0702417419437,21.6834532300656,19.5332802759701));
#143580=CARTESIAN_POINT('Ctrl Pts',(18.1542895053988,21.7060168103939,19.5375964387177));
#143581=CARTESIAN_POINT('Ctrl Pts',(18.2394591140179,21.724281910891,19.5419126014652));
#143582=CARTESIAN_POINT('Ctrl Pts',(18.3252730114509,21.7381609067947,19.5462287642128));
#143583=CARTESIAN_POINT('Ctrl Pts',(18.4082915298627,21.751587795812,19.5504043283958));
#143584=CARTESIAN_POINT('Ctrl Pts',(18.4919125329025,21.7609099414411,19.5545798925789));
#143585=CARTESIAN_POINT('Ctrl Pts',(18.5756985998726,21.7661009112592,19.5587554567619));
#143586=CARTESIAN_POINT('Ctrl Pts',(18.6637165024322,21.7715540646553,19.5631419187917));
#143587=CARTESIAN_POINT('Ctrl Pts',(18.7519159980506,21.7724477372193,19.5675283808216));
#143588=CARTESIAN_POINT('Ctrl Pts',(18.8397925195448,21.7688131172563,19.5719148428514));
#143589=CARTESIAN_POINT('Ctrl Pts',(18.9276690410391,21.7651784972933,19.5763013048812));
#143590=CARTESIAN_POINT('Ctrl Pts',(19.0152220177587,21.7570157144011,19.5806877669111));
#143591=CARTESIAN_POINT('Ctrl Pts',(19.1019580505816,21.7444180217667,19.5850742289409));
#143592=CARTESIAN_POINT('Ctrl Pts',(19.1847032324206,21.7323999672873,19.5892588634748));
#143593=CARTESIAN_POINT('Ctrl Pts',(19.2670129891846,21.7163014146095,19.5934434980088));
#143594=CARTESIAN_POINT('Ctrl Pts',(19.3484535429759,21.6961653553686,19.5976281325427));
#143595=CARTESIAN_POINT('Ctrl Pts',(19.4297781762334,21.6760579573122,19.6018068107681));
#143596=CARTESIAN_POINT('Ctrl Pts',(19.5102356212268,21.6519245772983,19.6059854889935));
#143597=CARTESIAN_POINT('Ctrl Pts',(19.5893993424999,21.6238597068315,19.6101641672189));
#143598=CARTESIAN_POINT('Ctrl Pts',(19.6699820131869,21.5952917949353,19.614417745069));
#143599=CARTESIAN_POINT('Ctrl Pts',(19.7492236469471,21.562650131979,19.6186713229191));
#143600=CARTESIAN_POINT('Ctrl Pts',(19.8266874127913,21.5260883823145,19.6229249007693));
#143601=CARTESIAN_POINT('Ctrl Pts',(19.9026493955877,21.490235451996,19.627096014889));
#143602=CARTESIAN_POINT('Ctrl Pts',(19.9769013948568,21.4506132807146,19.6312671290086));
#143603=CARTESIAN_POINT('Ctrl Pts',(20.0490505263125,21.4074157423505,19.6354382431283));
#143604=CARTESIAN_POINT('Ctrl Pts',(20.1211754474276,21.3642326993392,19.6396079575902));
#143605=CARTESIAN_POINT('Ctrl Pts',(20.1911985077687,21.3174769080841,19.6437776720521));
#143606=CARTESIAN_POINT('Ctrl Pts',(20.2587523619162,21.2673876664751,19.6479473865139));
#143607=CARTESIAN_POINT('Ctrl Pts',(20.3263038122014,21.2173002072608,19.6521169525991));
#143608=CARTESIAN_POINT('Ctrl Pts',(20.3913858619656,21.1638798082203,19.6562865186843));
#143609=CARTESIAN_POINT('Ctrl Pts',(20.4536621654798,21.1074076662515,19.6604560847694));
#143610=CARTESIAN_POINT('Ctrl Pts',(20.5181280223105,21.0489500376889,19.6647722473405));
#143611=CARTESIAN_POINT('Ctrl Pts',(20.5795867715906,20.9872224295952,19.6690884099116));
#143612=CARTESIAN_POINT('Ctrl Pts',(20.6377062426226,20.9225789616024,19.6734045724827));
#143613=CARTESIAN_POINT('Ctrl Pts',(20.6939324820534,20.8600412432703,19.6775801368131));
#143614=CARTESIAN_POINT('Ctrl Pts',(20.7470333951756,20.7947751107948,19.6817557011435));
#143615=CARTESIAN_POINT('Ctrl Pts',(20.7967499889561,20.7271340584069,19.6859312654739));
#143616=CARTESIAN_POINT('Ctrl Pts',(20.8489776441397,20.6560766248273,19.6903177271653));
#143617=CARTESIAN_POINT('Ctrl Pts',(20.8974697909607,20.5823985401433,19.6947041888567));
#143618=CARTESIAN_POINT('Ctrl Pts',(20.9419795412567,20.5065409470147,19.6990906505481));
#143619=CARTESIAN_POINT('Ctrl Pts',(20.9864892915527,20.4306833538862,19.7034771122395));
#143620=CARTESIAN_POINT('Ctrl Pts',(21.0270164454128,20.3526468022886,19.7078635739309));
#143621=CARTESIAN_POINT('Ctrl Pts',(21.0633723464503,20.2728966388461,19.7122500356223));
#143622=CARTESIAN_POINT('Ctrl Pts',(21.0980554588848,20.1968158979922,19.7164346697447));
#143623=CARTESIAN_POINT('Ctrl Pts',(21.1290718315298,20.1188925846167,19.7206193038671));
#143624=CARTESIAN_POINT('Ctrl Pts',(21.1562228177911,20.0395147077584,19.7248039379896));
#143625=CARTESIAN_POINT('Ctrl Pts',(21.1833351579832,19.9602498154855,19.7289826158031));
#143626=CARTESIAN_POINT('Ctrl Pts',(21.2065928926838,19.8795349037293,19.7331612936167));
#143627=CARTESIAN_POINT('Ctrl Pts',(21.2258445987322,19.797779767689,19.7373399714302));
#143628=CARTESIAN_POINT('Ctrl Pts',(21.2454413793552,19.7145592228834,19.7415935493833));
#143629=CARTESIAN_POINT('Ctrl Pts',(21.2608869019344,19.6302612334803,19.7458471273363));
#143630=CARTESIAN_POINT('Ctrl Pts',(21.2720739254944,19.5453362808994,19.7501007052894));
#143631=CARTESIAN_POINT('Ctrl Pts',(21.283044065894,19.4620577709145,19.7542718189995));
#143632=CARTESIAN_POINT('Ctrl Pts',(21.2899192902207,19.3781768678188,19.7584429327095));
#143633=CARTESIAN_POINT('Ctrl Pts',(21.2926499549084,19.2941288653065,19.7626140464196));
#143634=CARTESIAN_POINT('Ctrl Pts',(21.2953797032962,19.2101090658848,19.7667837604736));
#143635=CARTESIAN_POINT('Ctrl Pts',(21.2939676391619,19.1259227378138,19.7709534745275));
#143636=CARTESIAN_POINT('Ctrl Pts',(21.2884161370472,19.0420082877982,19.7751231885815));
#143637=CARTESIAN_POINT('Ctrl Pts',(21.2828648324763,18.958096823782,19.779292754261));
#143638=CARTESIAN_POINT('Ctrl Pts',(21.2731744140079,18.8744576775594,19.7834623199405));
#143639=CARTESIAN_POINT('Ctrl Pts',(21.2593992661634,18.7915258691394,19.78763188562));
#143640=CARTESIAN_POINT('Ctrl Pts',(21.2451397991587,18.7056782688699,19.791948048677));
#143641=CARTESIAN_POINT('Ctrl Pts',(21.2265031054902,18.620589192361,19.796264211734));
#143642=CARTESIAN_POINT('Ctrl Pts',(21.2036071461028,18.5367296210585,19.800580374791));
#143643=CARTESIAN_POINT('Ctrl Pts',(21.1814570231814,18.4556017774482,19.8047559387253));
#143644=CARTESIAN_POINT('Ctrl Pts',(21.1553210566048,18.3756249996566,19.8089315026597));
#143645=CARTESIAN_POINT('Ctrl Pts',(21.1253562910671,18.2972083994839,19.8131070665941));
#143646=CARTESIAN_POINT('Ctrl Pts',(21.09387807017,18.2148311468024,19.8174935292124));
#143647=CARTESIAN_POINT('Ctrl Pts',(21.0581743347953,18.1341763575253,19.8218799918307));
#143648=CARTESIAN_POINT('Ctrl Pts',(21.0184823804552,18.0556904079903,19.8262664544489));
#143649=CARTESIAN_POINT('Ctrl Pts',(20.9787904261151,17.9772044584552,19.8306529170672));
#143650=CARTESIAN_POINT('Ctrl Pts',(20.9351106070445,17.9008878144474,19.8350393796855));
#143651=CARTESIAN_POINT('Ctrl Pts',(20.8877320902706,17.827150989689,19.8394258423038));
#143652=CARTESIAN_POINT('Ctrl Pts',(20.8425432910205,17.7568220980682,19.8436095735004));
#143653=CARTESIAN_POINT('Ctrl Pts',(20.7938219698918,17.6885781039191,19.847793304697));
#143654=CARTESIAN_POINT('Ctrl Pts',(20.7417867108851,17.6227958180407,19.8519770358936));
#143655=CARTESIAN_POINT('Ctrl Pts',(20.6898163394592,17.5570955621832,19.8561555500085));
#143656=CARTESIAN_POINT('Ctrl Pts',(20.6345405135866,17.4938512802473,19.8603340641234));
#143657=CARTESIAN_POINT('Ctrl Pts',(20.5762218026546,17.4334120753606,19.8645125782384));
#143658=CARTESIAN_POINT('Ctrl Pts',(20.5179688787998,17.373041049598,19.8686863787335));
#143659=CARTESIAN_POINT('Ctrl Pts',(20.456680209176,17.3154691416453,19.8728601792286));
#143660=CARTESIAN_POINT('Ctrl Pts',(20.3926584428866,17.2610122641819,19.8770339797238));
#143661=CARTESIAN_POINT('Ctrl Pts',(20.3603008400853,17.2334889059104,19.8791434838256));
#143662=CARTESIAN_POINT('Ctrl Pts',(20.3272457056729,17.2067607242114,19.8812529879274));
#143663=CARTESIAN_POINT('Ctrl Pts',(20.2935357313021,17.1808649545432,19.8833624920292));
#143664=CARTESIAN_POINT('Origin',(18.734,19.211,-1.76670989022852));
#143665=CARTESIAN_POINT('',(20.2935357313021,17.1808649545431,20.7499611463308));
#143666=CARTESIAN_POINT('',(20.2916962192317,17.183223495321,20.6832232112625));
#143667=CARTESIAN_POINT('',(20.2935357313021,17.1808649545432,-1.76670989022852));
#143668=CARTESIAN_POINT('',(16.1740004726297,19.2094444088938,20.2332901098006));
#143669=CARTESIAN_POINT('Ctrl Pts',(16.1740004726297,19.2094444088938,20.2332901098006));
#143670=CARTESIAN_POINT('Ctrl Pts',(16.1739502760983,19.2920516545602,20.2374173417146));
#143671=CARTESIAN_POINT('Ctrl Pts',(16.1779027082651,19.3748187791154,20.2415445736285));
#143672=CARTESIAN_POINT('Ctrl Pts',(16.1858778001794,19.4573194161684,20.2456718055424));
#143673=CARTESIAN_POINT('Ctrl Pts',(16.1940130436991,19.5414767876655,20.249881918359));
#143674=CARTESIAN_POINT('Ctrl Pts',(16.2063343518328,19.6253563595504,20.2540920311757));
#143675=CARTESIAN_POINT('Ctrl Pts',(16.222807033423,19.7085036528651,20.2583021439923));
#143676=CARTESIAN_POINT('Ctrl Pts',(16.2389199317254,19.7898349087365,20.2624203028533));
#143677=CARTESIAN_POINT('Ctrl Pts',(16.2590046102348,19.8704650577792,20.2665384617144));
#143678=CARTESIAN_POINT('Ctrl Pts',(16.2829763020121,19.9499741753957,20.2706566205754));
#143679=CARTESIAN_POINT('Ctrl Pts',(16.3069370246241,20.0294469105714,20.2747728950152));
#143680=CARTESIAN_POINT('Ctrl Pts',(16.334781094809,20.1077991798405,20.278889169455));
#143681=CARTESIAN_POINT('Ctrl Pts',(16.3663732871992,20.1846240284793,20.2830054438948));
#143682=CARTESIAN_POINT('Ctrl Pts',(16.3979610861523,20.2614381933028,20.2871211458959));
#143683=CARTESIAN_POINT('Ctrl Pts',(16.4332957916267,20.3367249220046,20.291236847897));
#143684=CARTESIAN_POINT('Ctrl Pts',(16.4721937795329,20.4100965853743,20.2953525498981));
#143685=CARTESIAN_POINT('Ctrl Pts',(16.5126461135564,20.4864001474415,20.2996327135017));
#143686=CARTESIAN_POINT('Ctrl Pts',(16.5569522565608,20.5606318773211,20.3039128771053));
#143687=CARTESIAN_POINT('Ctrl Pts',(16.6048536565745,20.6323851864564,20.3081930407089));
#143688=CARTESIAN_POINT('Ctrl Pts',(16.6509736168395,20.7014700099742,20.3123140262181));
#143689=CARTESIAN_POINT('Ctrl Pts',(16.700425807859,20.7682571429841,20.3164350117273));
#143690=CARTESIAN_POINT('Ctrl Pts',(16.7529371454851,20.832416037438,20.3205559972365));
#143691=CARTESIAN_POINT('Ctrl Pts',(16.8054841275711,20.8966184826611,20.3246797800521));
#143692=CARTESIAN_POINT('Ctrl Pts',(16.8610940675905,20.9581887928557,20.3288035628677));
#143693=CARTESIAN_POINT('Ctrl Pts',(16.9194565998598,21.0168328408266,20.3329273456833));
#143694=CARTESIAN_POINT('Ctrl Pts',(16.9779086865543,21.0755668751946,20.3370574562401));
#143695=CARTESIAN_POINT('Ctrl Pts',(17.0391214360201,21.1313653808553,20.3411875667969));
#143696=CARTESIAN_POINT('Ctrl Pts',(17.102751683912,21.1839746402982,20.3453176773537));
#143697=CARTESIAN_POINT('Ctrl Pts',(17.1099251002331,21.189905595038,20.3457832892829));
#143698=CARTESIAN_POINT('Ctrl Pts',(17.1171292123955,21.1957960624817,20.3462489012121));
#143699=CARTESIAN_POINT('Ctrl Pts',(17.1243635072226,21.201645714616,20.3467145131413));
#143700=CARTESIAN_POINT('Ctrl Pts',(17.189381078246,21.254218934563,20.3508991582794));
#143701=CARTESIAN_POINT('Ctrl Pts',(17.2570980356913,21.3037012786361,20.3550838034176));
#143702=CARTESIAN_POINT('Ctrl Pts',(17.3271882231611,21.349803549779,20.3592684485557));
#143703=CARTESIAN_POINT('Ctrl Pts',(17.3971786443956,21.3958401990397,20.3634471372781));
#143704=CARTESIAN_POINT('Ctrl Pts',(17.469535204727,21.4385060812658,20.3676258260006));
#143705=CARTESIAN_POINT('Ctrl Pts',(17.5438988654553,21.477552291379,20.371804514723));
#143706=CARTESIAN_POINT('Ctrl Pts',(17.619595201075,21.5172982505808,20.3760580899355));
#143707=CARTESIAN_POINT('Ctrl Pts',(17.6973709112596,21.5532932167484,20.380311665148));
#143708=CARTESIAN_POINT('Ctrl Pts',(17.7768165359119,21.5853209168257,20.3845652403605));
#143709=CARTESIAN_POINT('Ctrl Pts',(17.8547221935262,21.6167277947667,20.3887363646432));
#143710=CARTESIAN_POINT('Ctrl Pts',(17.9342331579703,21.6443196566906,20.3929074889259));
#143711=CARTESIAN_POINT('Ctrl Pts',(18.0149402978302,21.6679397926517,20.3970786132086));
#143712=CARTESIAN_POINT('Ctrl Pts',(18.0956203528785,21.6915520018428,20.401248337688));
#143713=CARTESIAN_POINT('Ctrl Pts',(18.1774953449549,21.711195003098,20.4054180621675));
#143714=CARTESIAN_POINT('Ctrl Pts',(18.2601401458989,21.7267616816128,20.409587786647));
#143715=CARTESIAN_POINT('Ctrl Pts',(18.3427820028614,21.7423278056098,20.4137573625921));
#143716=CARTESIAN_POINT('Ctrl Pts',(18.4261931619305,21.7538178112606,20.4179269385372));
#143717=CARTESIAN_POINT('Ctrl Pts',(18.5099387942264,21.7611757931694,20.4220965144823));
#143718=CARTESIAN_POINT('Ctrl Pts',(18.5966283647877,21.7687924326811,20.4264126649273));
#143719=CARTESIAN_POINT('Ctrl Pts',(18.6836758371975,21.7719810786796,20.4307288153724));
#143720=CARTESIAN_POINT('Ctrl Pts',(18.7705956997401,21.7707384152996,20.4350449658174));
#143721=CARTESIAN_POINT('Ctrl Pts',(18.8546845879267,21.7695362253863,20.4392205395189));
#143722=CARTESIAN_POINT('Ctrl Pts',(18.9386535840454,21.7641870268946,20.4433961132204));
#143723=CARTESIAN_POINT('Ctrl Pts',(19.0220673263575,21.7547407917249,20.4475716869219));
#143724=CARTESIAN_POINT('Ctrl Pts',(19.1096934355563,21.7448175247481,20.4519581257387));
#143725=CARTESIAN_POINT('Ctrl Pts',(19.1967061584005,21.7303726255243,20.4563445645555));
#143726=CARTESIAN_POINT('Ctrl Pts',(19.2826140302886,21.7115244741395,20.4607310033723));
#143727=CARTESIAN_POINT('Ctrl Pts',(19.3685219021767,21.6926763227546,20.4651174421892));
#143728=CARTESIAN_POINT('Ctrl Pts',(19.4533243836773,21.6694251459735,20.469503881006));
#143729=CARTESIAN_POINT('Ctrl Pts',(19.5365517912822,21.6419485026034,20.4738903198228));
#143730=CARTESIAN_POINT('Ctrl Pts',(19.6159508693926,21.6157357414958,20.4780749893718));
#143731=CARTESIAN_POINT('Ctrl Pts',(19.6942121038407,21.5855801437023,20.4822596589207));
#143732=CARTESIAN_POINT('Ctrl Pts',(19.770915780013,21.551599424327,20.4864443284697));
#143733=CARTESIAN_POINT('Ctrl Pts',(19.8475102835633,21.5176670698335,20.4906230419632));
#143734=CARTESIAN_POINT('Ctrl Pts',(19.9225512152564,21.4799205926128,20.4948017554568));
#143735=CARTESIAN_POINT('Ctrl Pts',(19.9956349417348,21.4385271656691,20.4989804689503));
#143736=CARTESIAN_POINT('Ctrl Pts',(20.0700278568189,21.3963922357189,20.5032340380151));
#143737=CARTESIAN_POINT('Ctrl Pts',(20.1423922957485,21.3504785578701,20.5074876070798));
#143738=CARTESIAN_POINT('Ctrl Pts',(20.2123247807266,21.3010133594524,20.5117411761446));
#143739=CARTESIAN_POINT('Ctrl Pts',(20.2809022183518,21.2525066238464,20.5159123258944));
#143740=CARTESIAN_POINT('Ctrl Pts',(20.3471407141715,21.2005850501782,20.5200834756442));
#143741=CARTESIAN_POINT('Ctrl Pts',(20.4106870428273,21.1455078341571,20.5242546253941));
#143742=CARTESIAN_POINT('Ctrl Pts',(20.4742120489457,21.0904490989203,20.528424375543));
#143743=CARTESIAN_POINT('Ctrl Pts',(20.5350463346099,21.032237125278,20.532594125692));
#143744=CARTESIAN_POINT('Ctrl Pts',(20.5928697176814,20.9711714043487,20.536763875841));
#143745=CARTESIAN_POINT('Ctrl Pts',(20.650691043295,20.9101078562456,20.5409334776229));
#143746=CARTESIAN_POINT('Ctrl Pts',(20.705501363646,20.8461910973649,20.5451030794048));
#143747=CARTESIAN_POINT('Ctrl Pts',(20.7570183049857,20.7797564940719,20.5492726811867));
#143748=CARTESIAN_POINT('Ctrl Pts',(20.8103455374923,20.7109873970688,20.5535888016298));
#143749=CARTESIAN_POINT('Ctrl Pts',(20.8601432984269,20.639520622689,20.557904922073));
#143750=CARTESIAN_POINT('Ctrl Pts',(20.9061460099819,20.5657626033071,20.5622210425161));
#143751=CARTESIAN_POINT('Ctrl Pts',(20.9506510024677,20.4944059378543,20.5663966422013));
#143752=CARTESIAN_POINT('Ctrl Pts',(20.9916040779513,20.4209053655083,20.5705722418866));
#143753=CARTESIAN_POINT('Ctrl Pts',(21.0288115998389,20.3456540094871,20.5747478415718));
#143754=CARTESIAN_POINT('Ctrl Pts',(21.0678973294938,20.2666040215169,20.5791342223939));
#143755=CARTESIAN_POINT('Ctrl Pts',(21.1028491780513,20.185622378127,20.583520603216));
#143756=CARTESIAN_POINT('Ctrl Pts',(21.1335006707343,20.1031863769111,20.5879069840381));
#143757=CARTESIAN_POINT('Ctrl Pts',(21.1641521634173,20.0207503756951,20.5922933648601));
#143758=CARTESIAN_POINT('Ctrl Pts',(21.190503198923,19.9368605929086,20.5966797456822));
#143759=CARTESIAN_POINT('Ctrl Pts',(21.2124488472496,19.8520080432935,20.6010661265043));
#143760=CARTESIAN_POINT('Ctrl Pts',(21.2333845649191,19.7710603767749,20.6052506476957));
#143761=CARTESIAN_POINT('Ctrl Pts',(21.2503893834586,19.6889352855203,20.6094351688871));
#143762=CARTESIAN_POINT('Ctrl Pts',(21.2633350895848,19.6060493698199,20.6136196900785));
#143763=CARTESIAN_POINT('Ctrl Pts',(21.2762623681897,19.5232814377935,20.6177982548275));
#143764=CARTESIAN_POINT('Ctrl Pts',(21.2851419407632,19.4397552831427,20.6219768195765));
#143765=CARTESIAN_POINT('Ctrl Pts',(21.2898958841357,19.3559007572727,20.6261553843255));
#143766=CARTESIAN_POINT('Ctrl Pts',(21.294735201995,19.2705403158831,20.630408990528));
#143767=CARTESIAN_POINT('Ctrl Pts',(21.2952991221744,19.1848400591972,20.6346625967305));
#143768=CARTESIAN_POINT('Ctrl Pts',(21.291560298618,19.0992622761417,20.638916202933));
#143769=CARTESIAN_POINT('Ctrl Pts',(21.2878940830536,19.015346414515,20.6430872040592));
#143770=CARTESIAN_POINT('Ctrl Pts',(21.2800907693894,18.9315487929963,20.6472582051854));
#143771=CARTESIAN_POINT('Ctrl Pts',(21.2681770979566,18.848306691277,20.6514292063116));
#143772=CARTESIAN_POINT('Ctrl Pts',(21.2562674231734,18.7650925145781,20.6555988082025));
#143773=CARTESIAN_POINT('Ctrl Pts',(21.2402501942426,18.6824339426084,20.6597684100934));
#143774=CARTESIAN_POINT('Ctrl Pts',(21.2202039193129,18.6007622827183,20.6639380119843));
#143775=CARTESIAN_POINT('Ctrl Pts',(21.200158355009,18.5190935180289,20.6681074660658));
#143776=CARTESIAN_POINT('Ctrl Pts',(21.1760841391767,18.4384120424545,20.6722769201474));
#143777=CARTESIAN_POINT('Ctrl Pts',(21.1481104103813,18.3591367912108,20.6764463742289));
#143778=CARTESIAN_POINT('Ctrl Pts',(21.1191514849296,18.2770695735106,20.6807626708086));
#143779=CARTESIAN_POINT('Ctrl Pts',(21.0860134223638,18.1965099777348,20.6850789673884));
#143780=CARTESIAN_POINT('Ctrl Pts',(21.0488942540617,18.1179013802442,20.6893952639681));
#143781=CARTESIAN_POINT('Ctrl Pts',(21.0129862924117,18.0418577986347,20.693570718838));
#143782=CARTESIAN_POINT('Ctrl Pts',(20.9733533011739,17.9676402439561,20.697746173708));
#143783=CARTESIAN_POINT('Ctrl Pts',(20.9302210181299,17.895624297197,20.7019216285779));
#143784=CARTESIAN_POINT('Ctrl Pts',(20.8849064011797,17.8199646100351,20.7063083460125));
#143785=CARTESIAN_POINT('Ctrl Pts',(20.8357293767457,17.7467356778435,20.7106950634472));
#143786=CARTESIAN_POINT('Ctrl Pts',(20.7830012664589,17.6763359292504,20.7150817808818));
#143787=CARTESIAN_POINT('Ctrl Pts',(20.7302731561721,17.6059361806573,20.7194684983164));
#143788=CARTESIAN_POINT('Ctrl Pts',(20.6739943900424,17.5383660129748,20.723855215751));
#143789=CARTESIAN_POINT('Ctrl Pts',(20.6145211534981,17.4739795075341,20.7282419331856));
#143790=CARTESIAN_POINT('Ctrl Pts',(20.5577980728116,17.4125703568735,20.7324258004418));
#143791=CARTESIAN_POINT('Ctrl Pts',(20.497958300527,17.3538283604302,20.7366096676979));
#143792=CARTESIAN_POINT('Ctrl Pts',(20.4352825901188,17.2980866332845,20.740793534954));
#143793=CARTESIAN_POINT('Ctrl Pts',(20.3895046434955,17.2573732246395,20.7438494054129));
#143794=CARTESIAN_POINT('Ctrl Pts',(20.3422147220435,17.2182598192813,20.7469052758719));
#143795=CARTESIAN_POINT('Ctrl Pts',(20.2935357313021,17.1808649545431,20.7499611463308));
#143796=CARTESIAN_POINT('Ctrl Pts',(20.2935357313021,17.1808649545432,19.9498236335591));
#143797=CARTESIAN_POINT('Ctrl Pts',(20.2269623905211,17.1297237735993,19.9540083609104));
#143798=CARTESIAN_POINT('Ctrl Pts',(20.1579647730342,17.081932789023,19.9581930882618));
#143799=CARTESIAN_POINT('Ctrl Pts',(20.0869226296604,17.0377074844483,19.9623778156132));
#143800=CARTESIAN_POINT('Ctrl Pts',(20.0710253698527,17.0278110888231,19.9633142414411));
#143801=CARTESIAN_POINT('Ctrl Pts',(20.0550258220092,17.0180930547612,19.9642506672691));
#143802=CARTESIAN_POINT('Ctrl Pts',(20.0389283877504,17.0085554711087,19.965187093097));
#143803=CARTESIAN_POINT('Ctrl Pts',(19.9669932812562,16.9659345735974,19.9693717283982));
#143804=CARTESIAN_POINT('Ctrl Pts',(19.8928340180633,16.9267623273783,19.9735563636994));
#143805=CARTESIAN_POINT('Ctrl Pts',(19.8168151370682,16.8912777366814,19.9777409990006));
#143806=CARTESIAN_POINT('Ctrl Pts',(19.7409044598177,16.8558436540364,19.9819196779762));
#143807=CARTESIAN_POINT('Ctrl Pts',(19.6631398357153,16.8240869937955,19.9860983569517));
#143808=CARTESIAN_POINT('Ctrl Pts',(19.5839125153273,16.796202137592,19.9902770359273));
#143809=CARTESIAN_POINT('Ctrl Pts',(19.5032651236343,16.7678174729394,19.9945306135878));
#143810=CARTESIAN_POINT('Ctrl Pts',(19.4211024978258,16.7434450253959,19.9987841912482));
#143811=CARTESIAN_POINT('Ctrl Pts',(19.337861066102,16.7232395989874,20.0030377689087));
#143812=CARTESIAN_POINT('Ctrl Pts',(19.2562334111056,16.7034258891344,20.0072088837319));
#143813=CARTESIAN_POINT('Ctrl Pts',(19.1735688735385,16.6876191861435,20.0113799985551));
#143814=CARTESIAN_POINT('Ctrl Pts',(19.0902949413653,16.6759154028401,20.0155511133783));
#143815=CARTESIAN_POINT('Ctrl Pts',(19.0070489529371,16.6642155469066,20.019720828525));
#143816=CARTESIAN_POINT('Ctrl Pts',(18.9231944312015,16.6566159403015,20.0238905436717));
#143817=CARTESIAN_POINT('Ctrl Pts',(18.8391675225352,16.6531611090212,20.0280602588184));
#143818=CARTESIAN_POINT('Ctrl Pts',(18.7551436043077,16.649706400695,20.0322298255688));
#143819=CARTESIAN_POINT('Ctrl Pts',(18.6709477710271,16.6503961924556,20.0363993923192));
#143820=CARTESIAN_POINT('Ctrl Pts',(18.5870183641888,16.6552229364175,20.0405689590696));
#143821=CARTESIAN_POINT('Ctrl Pts',(18.500138140141,16.6602193806036,20.0448851207954));
#143822=CARTESIAN_POINT('Ctrl Pts',(18.4135439525353,16.6696490660532,20.0492012825211));
#143823=CARTESIAN_POINT('Ctrl Pts',(18.3277166966719,16.6834450792442,20.0535174442468));
#143824=CARTESIAN_POINT('Ctrl Pts',(18.2446852202539,16.696791694284,20.0576930091876));
#143825=CARTESIAN_POINT('Ctrl Pts',(18.1623719289201,16.7142243989078,20.0618685741284));
#143826=CARTESIAN_POINT('Ctrl Pts',(18.0812003839193,16.7356308030427,20.0660441390692));
#143827=CARTESIAN_POINT('Ctrl Pts',(17.9959291092702,16.7581183800159,20.0704305991874));
#143828=CARTESIAN_POINT('Ctrl Pts',(17.9119185059183,16.7849914459601,20.0748170593056));
#143829=CARTESIAN_POINT('Ctrl Pts',(17.8296377675515,16.8160618061167,20.0792035194238));
#143830=CARTESIAN_POINT('Ctrl Pts',(17.7473570291847,16.8471321662734,20.0835899795421));
#143831=CARTESIAN_POINT('Ctrl Pts',(17.6668066567997,16.8823995182561,20.0879764396603));
#143832=CARTESIAN_POINT('Ctrl Pts',(17.5884257348687,16.9216202580024,20.0923628997785));
#143833=CARTESIAN_POINT('Ctrl Pts',(17.5136510990685,16.9590364615644,20.0965475399908));
#143834=CARTESIAN_POINT('Ctrl Pts',(17.44057234666,17.0001895266255,20.1007321802031));
#143835=CARTESIAN_POINT('Ctrl Pts',(17.369587760884,17.0449023009683,20.1049168204155));
#143836=CARTESIAN_POINT('Ctrl Pts',(17.2987042121717,17.0895514326572,20.1090955043522));
#143837=CARTESIAN_POINT('Ctrl Pts',(17.2299092952701,17.1377499663397,20.1132741882888));
#143838=CARTESIAN_POINT('Ctrl Pts',(17.1635782312953,17.1892741361949,20.1174528722255));
#143839=CARTESIAN_POINT('Ctrl Pts',(17.0960583483994,17.241721748316,20.1217064486519));
#143840=CARTESIAN_POINT('Ctrl Pts',(17.0310919386145,17.2976151655664,20.1259600250784));
#143841=CARTESIAN_POINT('Ctrl Pts',(16.969045396673,17.3566712135668,20.1302136015048));
#143842=CARTESIAN_POINT('Ctrl Pts',(16.9082016412034,17.4145824465075,20.1343847213749));
#143843=CARTESIAN_POINT('Ctrl Pts',(16.8501659076493,17.4755344558904,20.138555841245));
#143844=CARTESIAN_POINT('Ctrl Pts',(16.7952502349704,17.5392197068402,20.142726961115));
#143845=CARTESIAN_POINT('Ctrl Pts',(16.7403529897255,17.6028835876472,20.1468966813293));
#143846=CARTESIAN_POINT('Ctrl Pts',(16.6885740262376,17.6692785404175,20.1510664015437));
#143847=CARTESIAN_POINT('Ctrl Pts',(16.6401868618722,17.7380619352452,20.155236121758));
#143848=CARTESIAN_POINT('Ctrl Pts',(16.5918014193961,17.8068428823705,20.1594056935901));
#143849=CARTESIAN_POINT('Ctrl Pts',(16.5468078000507,17.8780117258147,20.1635752654222));
#143850=CARTESIAN_POINT('Ctrl Pts',(16.5054369234628,17.9511958033507,20.1677448372542));
#143851=CARTESIAN_POINT('Ctrl Pts',(16.462611627541,18.0269527134222,20.1720609930214));
#143852=CARTESIAN_POINT('Ctrl Pts',(16.4236688015505,18.104868733296,20.1763771487885));
#143853=CARTESIAN_POINT('Ctrl Pts',(16.3888124800775,18.1845032896303,20.1806933045556));
#143854=CARTESIAN_POINT('Ctrl Pts',(16.3550914981959,18.2615439903646,20.1848688745605));
#143855=CARTESIAN_POINT('Ctrl Pts',(16.3251950198591,18.3401925369042,20.1890444445653));
#143856=CARTESIAN_POINT('Ctrl Pts',(16.2992578088608,18.4200319458494,20.1932200145702));
#143857=CARTESIAN_POINT('Ctrl Pts',(16.2720106919424,18.5039034812422,20.1976064632185));
#143858=CARTESIAN_POINT('Ctrl Pts',(16.2491334314256,18.5890887659587,20.2019929118667));
#143859=CARTESIAN_POINT('Ctrl Pts',(16.2307217504257,18.6750914208485,20.206379360515));
#143860=CARTESIAN_POINT('Ctrl Pts',(16.2123100694257,18.7610940757384,20.2107658091633));
#143861=CARTESIAN_POINT('Ctrl Pts',(16.198363984864,18.8479135158795,20.2151522578116));
#143862=CARTESIAN_POINT('Ctrl Pts',(16.1889163328193,18.9350486871749,20.2195387064599));
#143863=CARTESIAN_POINT('Ctrl Pts',(16.1790436177041,19.0261041916152,20.2241225075637));
#143864=CARTESIAN_POINT('Ctrl Pts',(16.1740562221026,19.1176988529932,20.2287063086676));
#143865=CARTESIAN_POINT('Ctrl Pts',(16.17400047263,19.2094444083109,20.2332901097715));
#143866=CARTESIAN_POINT('',(16.1742339579337,19.2120076676078,20.1667099326005));
#143867=CARTESIAN_POINT('Ctrl Pts',(20.2935357313021,17.1808649545432,19.8833624920292));
#143868=CARTESIAN_POINT('Ctrl Pts',(20.2268945096768,17.1296716280032,19.8875327690168));
#143869=CARTESIAN_POINT('Ctrl Pts',(20.1576921849675,17.0817340977654,19.8917030460043));
#143870=CARTESIAN_POINT('Ctrl Pts',(20.0862835185508,17.0373097540229,19.8958733229919));
#143871=CARTESIAN_POINT('Ctrl Pts',(20.0148883970778,16.992893836782,19.9000428089526));
#143872=CARTESIAN_POINT('Ctrl Pts',(19.9412881559087,16.9519900249486,19.9042122949134));
#143873=CARTESIAN_POINT('Ctrl Pts',(19.8658657268991,16.9148118595657,19.9083817808741));
#143874=CARTESIAN_POINT('Ctrl Pts',(19.7904349794946,16.8776295937757,19.9125517266905));
#143875=CARTESIAN_POINT('Ctrl Pts',(19.7131820583974,16.8441739925523,19.916721672507));
#143876=CARTESIAN_POINT('Ctrl Pts',(19.6345123880327,16.8146115842795,19.9208916183234));
#143877=CARTESIAN_POINT('Ctrl Pts',(19.5557587743145,16.7850176318591,19.9250660136212));
#143878=CARTESIAN_POINT('Ctrl Pts',(19.4755858247082,16.7593253280965,19.929240408919));
#143879=CARTESIAN_POINT('Ctrl Pts',(19.3944162566998,16.7376519921599,19.9334148042169));
#143880=CARTESIAN_POINT('Ctrl Pts',(19.3132002871327,16.7159662664004,19.9375915858579));
#143881=CARTESIAN_POINT('Ctrl Pts',(19.2309870146835,16.6983041792189,19.941768367499));
#143882=CARTESIAN_POINT('Ctrl Pts',(19.1482091649662,16.6847318496133,19.94594514914));
#143883=CARTESIAN_POINT('Ctrl Pts',(19.0652902625141,16.6711363928764,19.9501290479806));
#143884=CARTESIAN_POINT('Ctrl Pts',(18.9818053188629,16.6616446617399,19.9543129468212));
#143885=CARTESIAN_POINT('Ctrl Pts',(18.8981916908115,16.6562708384902,19.9584968456618));
#143886=CARTESIAN_POINT('Ctrl Pts',(18.8442012195363,16.6528008868022,19.9611984467696));
#143887=CARTESIAN_POINT('Ctrl Pts',(18.7901571239054,16.6510468154871,19.9639000478774));
#143888=CARTESIAN_POINT('Ctrl Pts',(18.7361763184546,16.6510009250709,19.9666016489852));
#143889=CARTESIAN_POINT('Ctrl Pts',(18.6525629441495,16.6509298432758,19.970786284297));
#143890=CARTESIAN_POINT('Ctrl Pts',(18.5687904831979,16.6549593424975,19.9749709196088));
#143891=CARTESIAN_POINT('Ctrl Pts',(18.4852943718232,16.6631095960554,19.9791555549207));
#143892=CARTESIAN_POINT('Ctrl Pts',(18.4019171067169,16.6712482487469,19.9833342339277));
#143893=CARTESIAN_POINT('Ctrl Pts',(18.3188158638129,16.6834959609775,19.9875129129346));
#143894=CARTESIAN_POINT('Ctrl Pts',(18.2364263585556,16.6998209001866,19.9916915919416));
#143895=CARTESIAN_POINT('Ctrl Pts',(18.1525601036937,16.7164384476283,19.9959451695968));
#143896=CARTESIAN_POINT('Ctrl Pts',(18.0694318349778,16.7372808264266,20.0001987472521));
#143897=CARTESIAN_POINT('Ctrl Pts',(17.9874960098027,16.7622591413913,20.0044523249073));
#143898=CARTESIAN_POINT('Ctrl Pts',(17.9071486482808,16.7867532097478,20.0086234398121));
#143899=CARTESIAN_POINT('Ctrl Pts',(17.8279483681478,16.8152241408414,20.0127945547169));
#143900=CARTESIAN_POINT('Ctrl Pts',(17.750311955398,16.8475368987634,20.0169656696217));
#143901=CARTESIAN_POINT('Ctrl Pts',(17.6727015943016,16.8798388138251,20.0211353848683));
#143902=CARTESIAN_POINT('Ctrl Pts',(17.5966544827465,16.9159798187964,20.0253051001149));
#143903=CARTESIAN_POINT('Ctrl Pts',(17.5225687033401,16.9557762387131,20.0294748153615));
#143904=CARTESIAN_POINT('Ctrl Pts',(17.448485560255,16.9955712424856,20.03364438223));
#143905=CARTESIAN_POINT('Ctrl Pts',(17.3763640154123,17.039021184132,20.0378139490985));
#143906=CARTESIAN_POINT('Ctrl Pts',(17.306577534957,17.0858964481018,20.041983515967));
#143907=CARTESIAN_POINT('Ctrl Pts',(17.2343374823217,17.1344197654316,20.0462996776086));
#143908=CARTESIAN_POINT('Ctrl Pts',(17.164600186369,17.1866134577584,20.0506158392503));
#143909=CARTESIAN_POINT('Ctrl Pts',(17.0977455244308,17.2421751496947,20.0549320008919));
#143910=CARTESIAN_POINT('Ctrl Pts',(17.0330686155273,17.2959269507464,20.0591075659941));
#143911=CARTESIAN_POINT('Ctrl Pts',(16.9710897386949,17.3528303455362,20.0632831310963));
#143912=CARTESIAN_POINT('Ctrl Pts',(16.9121162724542,17.4125729975048,20.0674586961985));
#143913=CARTESIAN_POINT('Ctrl Pts',(16.8501642398151,17.475333065051,20.0718451561099));
#143914=CARTESIAN_POINT('Ctrl Pts',(16.7915295867846,17.5412263087857,20.0762316160212));
#143915=CARTESIAN_POINT('Ctrl Pts',(16.7365203854444,17.6098519152075,20.0806180759326));
#143916=CARTESIAN_POINT('Ctrl Pts',(16.6815111841042,17.6784775216293,20.085004535844));
#143917=CARTESIAN_POINT('Ctrl Pts',(16.6301277117767,17.749834975445,20.0893909957553));
#143918=CARTESIAN_POINT('Ctrl Pts',(16.5826239199814,17.8234910946867,20.0937774556667));
#143919=CARTESIAN_POINT('Ctrl Pts',(16.5362791661082,17.8953500892742,20.0980568909977));
#143920=CARTESIAN_POINT('Ctrl Pts',(16.4934601213733,17.96965463442,20.1023363263287));
#143921=CARTESIAN_POINT('Ctrl Pts',(16.4544271375725,18.0460332344294,20.1066157616597));
#143922=CARTESIAN_POINT('Ctrl Pts',(16.4154575008457,18.1222878787389,20.1108882518464));
#143923=CARTESIAN_POINT('Ctrl Pts',(16.3802619050974,18.2006095046636,20.1151607420331));
#143924=CARTESIAN_POINT('Ctrl Pts',(16.3490570392734,18.2805984339648,20.1194332322197));
#143925=CARTESIAN_POINT('Ctrl Pts',(16.3179055659637,18.3604504996733,20.1236984120403));
#143926=CARTESIAN_POINT('Ctrl Pts',(16.2907313869123,18.4419637898502,20.1279635918609));
#143927=CARTESIAN_POINT('Ctrl Pts',(16.267704287416,18.5247161971242,20.1322287716815));
#143928=CARTESIAN_POINT('Ctrl Pts',(16.2447004012398,18.6073851827702,20.1364896518296));
#143929=CARTESIAN_POINT('Ctrl Pts',(16.2258353998839,18.6912903879612,20.1407505319778));
#143930=CARTESIAN_POINT('Ctrl Pts',(16.2112300227061,18.7759923659696,20.1450114121259));
#143931=CARTESIAN_POINT('Ctrl Pts',(16.1966372355967,18.8606213295208,20.1492686193273));
#143932=CARTESIAN_POINT('Ctrl Pts',(16.1862968405217,18.946045274463,20.1535258265288));
#143933=CARTESIAN_POINT('Ctrl Pts',(16.1802787590545,19.0318134392765,20.1577830337302));
#143934=CARTESIAN_POINT('Ctrl Pts',(16.1760723590125,19.0917619816882,20.160758652563));
#143935=CARTESIAN_POINT('Ctrl Pts',(16.1739765481557,19.1518784238251,20.1637342713957));
#143936=CARTESIAN_POINT('Ctrl Pts',(16.1740001980189,19.2120069046219,20.1667098902285));
#143937=CARTESIAN_POINT('Ctrl Pts',(16.1778405256925,19.2120194393453,20.1667105863375));
#143938=CARTESIAN_POINT('Ctrl Pts',(16.17655676437,19.5768333952661,20.1847914783409));
#143939=CARTESIAN_POINT('Ctrl Pts',(16.4202751262482,20.7953392457516,20.245264305905));
#143940=CARTESIAN_POINT('Ctrl Pts',(18.293812263991,22.2059164112385,20.3481290690295));
#143941=CARTESIAN_POINT('Ctrl Pts',(21.0139857695323,21.202220683841,20.4753048757109));
#143942=CARTESIAN_POINT('Ctrl Pts',(21.565931958902,18.716185413598,20.5870029231219));
#143943=CARTESIAN_POINT('Ctrl Pts',(20.719740363017,17.5166786165403,20.6563090349724));
#143944=CARTESIAN_POINT('Ctrl Pts',(20.2916962192318,17.1832234953211,20.6832232112625));
#143945=CARTESIAN_POINT('Origin',(18.734,19.211,-1.76670989022852));
#143946=CARTESIAN_POINT('',(20.2910035798173,17.1841778967012,21.5499225020685));
#143947=CARTESIAN_POINT('',(20.2957383339893,17.178031980842,21.4832513393832));
#143948=CARTESIAN_POINT('',(20.2935357313021,17.1808649545432,-1.76670989022852));
#143949=CARTESIAN_POINT('',(16.1741052590002,19.209658325614,21.0332900820446));
#143950=CARTESIAN_POINT('Ctrl Pts',(16.1775161339837,19.2096606725892,21.0332901097715));
#143951=CARTESIAN_POINT('Ctrl Pts',(16.1799699186122,19.7238724897518,21.0587831909243));
#143952=CARTESIAN_POINT('Ctrl Pts',(16.5801691862074,21.0966582496844,21.1266682076376));
#143953=CARTESIAN_POINT('Ctrl Pts',(18.8208064662072,22.2367206740717,21.2369451599114));
#143954=CARTESIAN_POINT('Ctrl Pts',(21.3254400167184,20.7760162000723,21.3641209665928));
#143955=CARTESIAN_POINT('Ctrl Pts',(21.4293000776619,18.3992335115625,21.4684467473119));
#143956=CARTESIAN_POINT('Ctrl Pts',(20.6042288382577,17.4236622121578,21.5303805924704));
#143957=CARTESIAN_POINT('Ctrl Pts',(20.2910035798173,17.1841778967012,21.5499225020685));
#143958=CARTESIAN_POINT('Ctrl Pts',(20.2935357313021,17.1808649545431,20.7499611463308));
#143959=CARTESIAN_POINT('Ctrl Pts',(20.2235403921486,17.1270950180659,20.7543551710615));
#143960=CARTESIAN_POINT('Ctrl Pts',(20.1506714606626,17.0768804970143,20.7587491957922));
#143961=CARTESIAN_POINT('Ctrl Pts',(20.0753314078174,17.0305344409043,20.7631432205228));
#143962=CARTESIAN_POINT('Ctrl Pts',(20.0038028427435,16.9865330529945,20.7673149495304));
#143963=CARTESIAN_POINT('Ctrl Pts',(19.9300475351787,16.9460185369239,20.7714866785379));
#143964=CARTESIAN_POINT('Ctrl Pts',(19.8544414196889,16.9092156866801,20.7756584075455));
#143965=CARTESIAN_POINT('Ctrl Pts',(19.7788660377839,16.8724277966484,20.7798284407618));
#143966=CARTESIAN_POINT('Ctrl Pts',(19.7014417550698,16.8393487774228,20.7839984739781));
#143967=CARTESIAN_POINT('Ctrl Pts',(19.6225688678681,16.8101573631211,20.7881685071945));
#143968=CARTESIAN_POINT('Ctrl Pts',(19.5437043851342,16.7809690593725,20.7923380960641));
#143969=CARTESIAN_POINT('Ctrl Pts',(19.463392036181,16.7556676965775,20.7965076849337));
#143970=CARTESIAN_POINT('Ctrl Pts',(19.3820505615475,16.7343832614476,20.8006772738032));
#143971=CARTESIAN_POINT('Ctrl Pts',(19.3006933573855,16.7130947104084,20.8048476689733));
#143972=CARTESIAN_POINT('Ctrl Pts',(19.2183070776701,16.6958247446206,20.8090180641433));
#143973=CARTESIAN_POINT('Ctrl Pts',(19.1353226944306,16.6826526949537,20.8131884593133));
#143974=CARTESIAN_POINT('Ctrl Pts',(19.0522458413061,16.6694659676104,20.8173635015742));
#143975=CARTESIAN_POINT('Ctrl Pts',(18.9685700096491,16.6603863408392,20.821538543835));
#143976=CARTESIAN_POINT('Ctrl Pts',(18.884732812933,16.6554414271817,20.8257135860958));
#143977=CARTESIAN_POINT('Ctrl Pts',(18.8008414473993,16.6504933185207,20.8298913259313));
#143978=CARTESIAN_POINT('Ctrl Pts',(18.7167889688217,16.6496852442149,20.8340690657669));
#143979=CARTESIAN_POINT('Ctrl Pts',(18.6330121303373,16.6529926798031,20.8382468056024));
#143980=CARTESIAN_POINT('Ctrl Pts',(18.5490995249123,16.6563054753502,20.8424313157932));
#143981=CARTESIAN_POINT('Ctrl Pts',(18.4654639082309,16.6637470495906,20.8466158259839));
#143982=CARTESIAN_POINT('Ctrl Pts',(18.3825355613592,16.6752411888409,20.8508003361747));
#143983=CARTESIAN_POINT('Ctrl Pts',(18.352033094117,16.6794689302488,20.8523394707388));
#143984=CARTESIAN_POINT('Ctrl Pts',(18.3216261951854,16.6842444455182,20.853878605303));
#143985=CARTESIAN_POINT('Ctrl Pts',(18.291335798662,16.6895622345864,20.8554177398671));
#143986=CARTESIAN_POINT('Ctrl Pts',(18.2089776381982,16.7040210524186,20.8596025742027));
#143987=CARTESIAN_POINT('Ctrl Pts',(18.1271754855616,16.7225461173931,20.8637874085383));
#143988=CARTESIAN_POINT('Ctrl Pts',(18.0463616920216,16.7450815996062,20.8679722428739));
#143989=CARTESIAN_POINT('Ctrl Pts',(17.9656628851169,16.7675850170052,20.8721511227802));
#143990=CARTESIAN_POINT('Ctrl Pts',(17.8859500832465,16.7940873946836,20.8763300026864));
#143991=CARTESIAN_POINT('Ctrl Pts',(17.807646872009,16.8244816400745,20.8805088825927));
#143992=CARTESIAN_POINT('Ctrl Pts',(17.7279449225123,16.855418820975,20.8847624102575));
#143993=CARTESIAN_POINT('Ctrl Pts',(17.6497038935229,16.8903881967177,20.8890159379224));
#143994=CARTESIAN_POINT('Ctrl Pts',(17.573355832904,16.929223254263,20.8932694655872));
#143995=CARTESIAN_POINT('Ctrl Pts',(17.4984833659801,16.96730773916,20.8974407845023));
#143996=CARTESIAN_POINT('Ctrl Pts',(17.4254317755321,17.0091095912712,20.9016121034175));
#143997=CARTESIAN_POINT('Ctrl Pts',(17.3545880686225,17.0544233786917,20.9057834223326));
#143998=CARTESIAN_POINT('Ctrl Pts',(17.2837681207943,17.0997219690819,20.9099533422992));
#143999=CARTESIAN_POINT('Ctrl Pts',(17.2151549730969,17.1485299079787,20.9141232622657));
#144000=CARTESIAN_POINT('Ctrl Pts',(17.1491087606968,17.2005971151085,20.9182931822322));
#144001=CARTESIAN_POINT('Ctrl Pts',(17.0830648915168,17.2526624749723,20.9224629542563));
#144002=CARTESIAN_POINT('Ctrl Pts',(17.0195881372629,17.3079865877146,20.9266327262803));
#144003=CARTESIAN_POINT('Ctrl Pts',(16.9590064076381,17.3662784093326,20.9308024983044));
#144004=CARTESIAN_POINT('Ctrl Pts',(16.8963013152172,17.4266133334852,20.9351184189914));
#144005=CARTESIAN_POINT('Ctrl Pts',(16.8366983378617,17.4901275013993,20.9394343396784));
#144006=CARTESIAN_POINT('Ctrl Pts',(16.7805189594492,17.5564572159631,20.9437502603654));
#144007=CARTESIAN_POINT('Ctrl Pts',(16.7261639013725,17.6206329969918,20.9479260295929));
#144008=CARTESIAN_POINT('Ctrl Pts',(16.6750137437496,17.6874438611066,20.9521017988205));
#144009=CARTESIAN_POINT('Ctrl Pts',(16.627316944944,17.7565287883427,20.956277568048));
#144010=CARTESIAN_POINT('Ctrl Pts',(16.5772188726481,17.8290917645988,20.9606635644648));
#144011=CARTESIAN_POINT('Ctrl Pts',(16.5309313071797,17.9041632904909,20.9650495608815));
#144012=CARTESIAN_POINT('Ctrl Pts',(16.4886879176914,17.9812952984399,20.9694355572982));
#144013=CARTESIAN_POINT('Ctrl Pts',(16.4464445282031,18.0584273063889,20.973821553715));
#144014=CARTESIAN_POINT('Ctrl Pts',(16.4082454981439,18.1376192412558,20.9782075501317));
#144015=CARTESIAN_POINT('Ctrl Pts',(16.3742656129549,18.2184005729416,20.9825935465485));
#144016=CARTESIAN_POINT('Ctrl Pts',(16.3382155097944,18.3041034917275,20.9872467589536));
#144017=CARTESIAN_POINT('Ctrl Pts',(16.306798874077,18.3918657738651,20.9918999713587));
#144018=CARTESIAN_POINT('Ctrl Pts',(16.2802296051744,18.4811980751755,20.9965531837637));
#144019=CARTESIAN_POINT('Ctrl Pts',(16.2537435497692,18.5702505926029,21.001191822562));
#144020=CARTESIAN_POINT('Ctrl Pts',(16.2320746945689,18.6608630689237,21.0058304613603));
#144021=CARTESIAN_POINT('Ctrl Pts',(16.2153886002422,18.752527953949,21.0104691001586));
#144022=CARTESIAN_POINT('Ctrl Pts',(16.1987928060345,18.8436967762135,21.0150826360402));
#144023=CARTESIAN_POINT('Ctrl Pts',(16.1871261070645,18.9359063886952,21.0196961719218));
#144024=CARTESIAN_POINT('Ctrl Pts',(16.1805035110245,19.0286385984106,21.0243097078035));
#144025=CARTESIAN_POINT('Ctrl Pts',(16.1762064897689,19.0888071899736,21.0273031655996));
#144026=CARTESIAN_POINT('Ctrl Pts',(16.1740320413884,19.1491954186321,21.0302966233957));
#144027=CARTESIAN_POINT('Ctrl Pts',(16.174000351618,19.2096582534287,21.0332900811918));
#144028=CARTESIAN_POINT('',(16.1715627854608,19.2128544306465,20.9667098902285));
#144029=CARTESIAN_POINT('Ctrl Pts',(20.2916962192318,17.1832234953211,20.6832232112625));
#144030=CARTESIAN_POINT('Ctrl Pts',(20.0455373123707,16.9914606845963,20.6987009705329));
#144031=CARTESIAN_POINT('Ctrl Pts',(19.0022218457995,16.4381424631027,20.7565706653639));
#144032=CARTESIAN_POINT('Ctrl Pts',(16.8944629772976,16.8838679918332,20.8510662250192));
#144033=CARTESIAN_POINT('Ctrl Pts',(16.1775450542205,18.4784656881504,20.9300840254041));
#144034=CARTESIAN_POINT('Ctrl Pts',(16.1715627854608,19.2128544306465,20.9667098902285));
#144035=CARTESIAN_POINT('Ctrl Pts',(16.1715627854608,19.2128544306465,20.9667098902285));
#144036=CARTESIAN_POINT('Ctrl Pts',(16.1706209869532,19.3284704702211,20.9724759609646));
#144037=CARTESIAN_POINT('Ctrl Pts',(16.2303035804914,20.2931122226394,21.0206339672611));
#144038=CARTESIAN_POINT('Ctrl Pts',(17.4553333859632,21.9547543997083,21.1111839091181));
#144039=CARTESIAN_POINT('Ctrl Pts',(20.3489604234473,21.7713501510339,21.2383597157995));
#144040=CARTESIAN_POINT('Ctrl Pts',(21.7259567294576,19.3016368932709,21.3623821925546));
#144041=CARTESIAN_POINT('Ctrl Pts',(20.9160604073402,17.6604732139873,21.4440127337491));
#144042=CARTESIAN_POINT('Ctrl Pts',(20.2957383339893,17.178031980842,21.4832513393832));
#144043=CARTESIAN_POINT('Origin',(18.734,-18.952,-1.76670989022851));
#144044=CARTESIAN_POINT('',(20.2955776483338,-20.9847559318741,0.749817810273507));
#144045=CARTESIAN_POINT('',(20.2916906430028,-20.9796979674239,0.683386616606776));
#144046=CARTESIAN_POINT('',(20.2935357468249,-20.9821350335323,-1.76670989022851));
#144047=CARTESIAN_POINT('',(16.1740007446509,-18.9500474088581,0.233290109771496));
#144048=CARTESIAN_POINT('Ctrl Pts',(16.1719919811635,-18.9500458767116,
0.233290109771496));
#144049=CARTESIAN_POINT('Ctrl Pts',(16.1708576376271,-18.8187090077496,
0.239839092339242));
#144050=CARTESIAN_POINT('Ctrl Pts',(16.2398215302323,-17.838374208454,0.288780010467466));
#144051=CARTESIAN_POINT('Ctrl Pts',(17.5061738910726,-16.184820909787,0.380112864156167));
#144052=CARTESIAN_POINT('Ctrl Pts',(20.3959079738877,-16.4220626898431,
0.507288670837602));
#144053=CARTESIAN_POINT('Ctrl Pts',(21.7186679417731,-18.9005846219903,
0.630523652876716));
#144054=CARTESIAN_POINT('Ctrl Pts',(20.9031377956339,-20.5111939695708,
0.711366699355352));
#144055=CARTESIAN_POINT('Ctrl Pts',(20.2955776483338,-20.9847559318741,
0.749817810273507));
#144056=CARTESIAN_POINT('',(19.3957675194894,-21.4249868075161,1.730088294849E-11));
#144057=CARTESIAN_POINT('Ctrl Pts',(19.3957675194894,-21.4249868075161,
1.73008274373387E-11));
#144058=CARTESIAN_POINT('Ctrl Pts',(19.3150528143647,-21.4465859402064,
0.00418159702990585));
#144059=CARTESIAN_POINT('Ctrl Pts',(19.2331283755591,-21.4642697491679,
0.0083631940425111));
#144060=CARTESIAN_POINT('Ctrl Pts',(19.1504091626665,-21.4779064529882,
0.0125447910551162));
#144061=CARTESIAN_POINT('Ctrl Pts',(19.0678077425558,-21.4915237380395,
0.0167204334420983));
#144062=CARTESIAN_POINT('Ctrl Pts',(18.9844142470727,-21.501105290632,0.0208960758290806));
#144063=CARTESIAN_POINT('Ctrl Pts',(18.9006573352602,-21.506569500445,0.0250717182160627));
#144064=CARTESIAN_POINT('Ctrl Pts',(18.8165041727153,-21.5120595612247,
0.029267115406781));
#144065=CARTESIAN_POINT('Ctrl Pts',(18.7319846004062,-21.5133930928997,
0.0334625125974991));
#144066=CARTESIAN_POINT('Ctrl Pts',(18.6475423362417,-21.5105396366634,
0.0376579097882175));
#144067=CARTESIAN_POINT('Ctrl Pts',(18.5636493303861,-21.5077047408548,
0.041826017838971));
#144068=CARTESIAN_POINT('Ctrl Pts',(18.4798330960835,-21.5007371781061,
0.0459941258897243));
#144069=CARTESIAN_POINT('Ctrl Pts',(18.3965306502634,-21.4896592438679,
0.0501622339404779));
#144070=CARTESIAN_POINT('Ctrl Pts',(18.3132562868314,-21.4785850441522,
0.0543289368652889));
#144071=CARTESIAN_POINT('Ctrl Pts',(18.2304958242585,-21.4634032856077,
0.0584956397901002));
#144072=CARTESIAN_POINT('Ctrl Pts',(18.1486808249577,-21.4441880874701,
0.0626623427149111));
#144073=CARTESIAN_POINT('Ctrl Pts',(18.0668687681529,-21.4249735804117,
0.0668288957832525));
#144074=CARTESIAN_POINT('Ctrl Pts',(17.9860025553434,-21.4017260285035,
0.0709954488515935));
#144075=CARTESIAN_POINT('Ctrl Pts',(17.9065018743522,-21.3745702986806,
0.0751620019199348));
#144076=CARTESIAN_POINT('Ctrl Pts',(17.8260461859792,-21.3470883587911,
0.0793786059927156));
#144077=CARTESIAN_POINT('Ctrl Pts',(17.7469895187101,-21.3156038569086,
0.0835952100654965));
#144078=CARTESIAN_POINT('Ctrl Pts',(17.6697476372837,-21.2802969974753,
0.0878118141382773));
#144079=CARTESIAN_POINT('Ctrl Pts',(17.5933153937669,-21.24536021929,0.0919842203944796));
#144080=CARTESIAN_POINT('Ctrl Pts',(17.5186604552654,-21.2066811083584,
0.0961566266506819));
#144081=CARTESIAN_POINT('Ctrl Pts',(17.4461606843492,-21.1644804851262,
0.100329032906884));
#144082=CARTESIAN_POINT('Ctrl Pts',(17.3725089409092,-21.1216093224172,
0.104567735887954));
#144083=CARTESIAN_POINT('Ctrl Pts',(17.3010818658164,-21.0751040329196,
0.108806438869025));
#144084=CARTESIAN_POINT('Ctrl Pts',(17.2322432557832,-21.0252406230824,
0.113045141850095));
#144085=CARTESIAN_POINT('Ctrl Pts',(17.1634046457499,-20.9753772132452,
0.117283844831166));
#144086=CARTESIAN_POINT('Ctrl Pts',(17.0971548434137,-20.922156041386,0.121522547812235));
#144087=CARTESIAN_POINT('Ctrl Pts',(17.0338195258261,-20.8658929842699,
0.125761250793306));
#144088=CARTESIAN_POINT('Ctrl Pts',(16.9721381141262,-20.8110991516714,
0.129889266466191));
#144089=CARTESIAN_POINT('Ctrl Pts',(16.9129812124539,-20.7532072684117,
0.134017282139077));
#144090=CARTESIAN_POINT('Ctrl Pts',(16.8566825230424,-20.6924824304513,
0.138145297811962));
#144091=CARTESIAN_POINT('Ctrl Pts',(16.8004749041019,-20.6318558228343,
0.142266635881243));
#144092=CARTESIAN_POINT('Ctrl Pts',(16.7471166297386,-20.5684057102785,
0.146387973950524));
#144093=CARTESIAN_POINT('Ctrl Pts',(16.6969071781283,-20.5024363369964,
0.150509312019806));
#144094=CARTESIAN_POINT('Ctrl Pts',(16.6467433529369,-20.4365269115162,
0.154626904939698));
#144095=CARTESIAN_POINT('Ctrl Pts',(16.5997229596986,-20.3681031412178,
0.158744497859592));
#144096=CARTESIAN_POINT('Ctrl Pts',(16.556106820746,-20.2975041061843,0.162862090779484));
#144097=CARTESIAN_POINT('Ctrl Pts',(16.5125163940206,-20.2269466901128,
0.166977256329893));
#144098=CARTESIAN_POINT('Ctrl Pts',(16.4723264872833,-20.1542169560892,
0.171092421880302));
#144099=CARTESIAN_POINT('Ctrl Pts',(16.4357550860861,-20.0796836061897,
0.175207587430711));
#144100=CARTESIAN_POINT('Ctrl Pts',(16.3991935731796,-20.005170408852,0.179321640309701));
#144101=CARTESIAN_POINT('Ctrl Pts',(16.3662488306016,-19.9288549893914,
0.18343569318869));
#144102=CARTESIAN_POINT('Ctrl Pts',(16.3370925482441,-19.8511299504059,
0.18754974606768));
#144103=CARTESIAN_POINT('Ctrl Pts',(16.3079200305593,-19.7733616311617,
0.191666089807838));
#144104=CARTESIAN_POINT('Ctrl Pts',(16.2825403576348,-19.694182567114,0.195782433547997));
#144105=CARTESIAN_POINT('Ctrl Pts',(16.2610764230542,-19.6140037632713,
0.199898777288155));
#144106=CARTESIAN_POINT('Ctrl Pts',(16.239606571648,-19.5338028570508,0.204016255754456));
#144107=CARTESIAN_POINT('Ctrl Pts',(16.2220547122219,-19.4526021247793,
0.208133734220756));
#144108=CARTESIAN_POINT('Ctrl Pts',(16.2084928022863,-19.3708238225034,
0.212251212687057));
#144109=CARTESIAN_POINT('Ctrl Pts',(16.1949128185011,-19.2889365349339,
0.216374178484198));
#144110=CARTESIAN_POINT('Ctrl Pts',(16.1853334601433,-19.2064706109328,
0.22049714428134));
#144111=CARTESIAN_POINT('Ctrl Pts',(16.1797748249049,-19.1238538766228,
0.224620110078481));
#144112=CARTESIAN_POINT('Ctrl Pts',(16.1758784900672,-19.0659435359969,
0.227510109976153));
#144113=CARTESIAN_POINT('Ctrl Pts',(16.1739565735353,-19.0079591859799,
0.230400109873824));
#144114=CARTESIAN_POINT('Ctrl Pts',(16.1740007446509,-18.9500474088581,
0.233290109771496));
#144115=CARTESIAN_POINT('',(18.0722627314315,-21.4249949024184,0.));
#144116=CARTESIAN_POINT('Origin',(18.734,-18.952,0.));
#144117=CARTESIAN_POINT('',(16.1765334791563,-18.9551432954109,0.166709890228505));
#144118=CARTESIAN_POINT('Ctrl Pts',(18.0722627314315,-21.4249949024184,
-8.32667268468867E-16));
#144119=CARTESIAN_POINT('Ctrl Pts',(17.2488902483963,-21.2046724677036,
0.0423919355604773));
#144120=CARTESIAN_POINT('Ctrl Pts',(16.3345567445347,-20.3367913268265,
0.0979618989699792));
#144121=CARTESIAN_POINT('Ctrl Pts',(16.174495607841,-19.2205924221476,0.153531862379481));
#144122=CARTESIAN_POINT('Ctrl Pts',(16.1765334791563,-18.9551432954109,
0.166709890228505));
#144123=CARTESIAN_POINT('Ctrl Pts',(16.1765334791563,-18.9551432954109,
0.166709890228505));
#144124=CARTESIAN_POINT('Ctrl Pts',(16.1810511645957,-18.366678437132,0.195923797939959));
#144125=CARTESIAN_POINT('Ctrl Pts',(16.6739009874383,-16.9152607583549,
0.267529641211892));
#144126=CARTESIAN_POINT('Ctrl Pts',(19.0860575095572,-15.9462785509947,
0.381527420044301));
#144127=CARTESIAN_POINT('Ctrl Pts',(21.4520483087009,-17.6196576192121,
0.508703226725736));
#144128=CARTESIAN_POINT('Ctrl Pts',(21.3518776905422,-19.9120072668099,
0.60932295891323));
#144129=CARTESIAN_POINT('Ctrl Pts',(20.5461545388389,-20.7868242253756,
0.667550755540244));
#144130=CARTESIAN_POINT('Ctrl Pts',(20.2916906430027,-20.979697967424,0.683386616606783));
#144131=CARTESIAN_POINT('Origin',(18.734,-18.952,-1.76670989022851));
#144132=CARTESIAN_POINT('',(20.2940723489731,-20.982845288132,1.55000082941896));
#144133=CARTESIAN_POINT('',(20.2935357468249,-20.9821350335323,1.48324950709828));
#144134=CARTESIAN_POINT('',(20.2935357468249,-20.9821350335323,-1.76670989022851));
#144135=CARTESIAN_POINT('',(16.1715629797346,-18.9538544393498,1.0332901097715));
#144136=CARTESIAN_POINT('Ctrl Pts',(16.1715629797346,-18.9538544393498,
1.0332901097715));
#144137=CARTESIAN_POINT('Ctrl Pts',(16.1775452476667,-18.2194657538418,
1.06991597459592));
#144138=CARTESIAN_POINT('Ctrl Pts',(16.8944631229174,-16.6248681563667,
1.14893377498083));
#144139=CARTESIAN_POINT('Ctrl Pts',(19.6025525643745,-16.052191380828,1.27034351092621));
#144140=CARTESIAN_POINT('Ctrl Pts',(21.6424137382259,-18.1127008887664,
1.39751931760764));
#144141=CARTESIAN_POINT('Ctrl Pts',(21.1817796643434,-20.1874548702378,
1.4907384237719));
#144142=CARTESIAN_POINT('Ctrl Pts',(20.4294541422046,-20.881008060679,1.54156559437567));
#144143=CARTESIAN_POINT('Ctrl Pts',(20.294072348973,-20.9828452881321,1.55000082941897));
#144144=CARTESIAN_POINT('Ctrl Pts',(20.2955776483338,-20.9847559318741,
0.749817810273507));
#144145=CARTESIAN_POINT('Ctrl Pts',(20.23330927837,-21.0332909314137,0.753758634915827));
#144146=CARTESIAN_POINT('Ctrl Pts',(19.4740834602792,-21.567801555079,0.800091395118626));
#144147=CARTESIAN_POINT('Ctrl Pts',(17.4553335005934,-21.6957541409811,
0.888816090881904));
#144148=CARTESIAN_POINT('Ctrl Pts',(16.230303771566,-20.0341121451265,0.979366032738913));
#144149=CARTESIAN_POINT('Ctrl Pts',(16.1706211813573,-19.0694704699527,
1.02752403903544));
#144150=CARTESIAN_POINT('Ctrl Pts',(16.1715629797346,-18.9538544393498,
1.0332901097715));
#144151=CARTESIAN_POINT('',(16.1740711676982,-18.9506582890571,0.966709918231089));
#144152=CARTESIAN_POINT('Ctrl Pts',(20.2916906430027,-20.979697967424,0.683386616606783));
#144153=CARTESIAN_POINT('Ctrl Pts',(19.8649653676639,-21.3031391393463,
0.709942691100723));
#144154=CARTESIAN_POINT('Ctrl Pts',(18.4990491243427,-21.814007150788,0.778890701155144));
#144155=CARTESIAN_POINT('Ctrl Pts',(16.5801690201362,-20.8376582933814,
0.873331792362383));
#144156=CARTESIAN_POINT('Ctrl Pts',(16.1799697387475,-19.4648724906692,
0.941216809075683));
#144157=CARTESIAN_POINT('Ctrl Pts',(16.1775159588735,-18.9506606593868,
0.966709890228505));
#144158=CARTESIAN_POINT('Ctrl Pts',(16.1740003516248,-18.9506582403292,
0.96670991880675));
#144159=CARTESIAN_POINT('Ctrl Pts',(16.1740492156647,-18.8574284856305,
0.971325636022637));
#144160=CARTESIAN_POINT('Ctrl Pts',(16.1791950640212,-18.7643768125493,
0.975941353238524));
#144161=CARTESIAN_POINT('Ctrl Pts',(16.1893550102722,-18.6720323657042,
0.980557070454411));
#144162=CARTESIAN_POINT('Ctrl Pts',(16.1995507619901,-18.57936248052,0.985189054282917));
#144163=CARTESIAN_POINT('Ctrl Pts',(16.2147958864483,-18.487405080462,0.989821038111424));
#144164=CARTESIAN_POINT('Ctrl Pts',(16.234956622384,-18.3966782943254,0.994453021939931));
#144165=CARTESIAN_POINT('Ctrl Pts',(16.25521618901,-18.3055067530499,0.999107712387932));
#144166=CARTESIAN_POINT('Ctrl Pts',(16.2804395488529,-18.2155781794355,
1.00376240283593));
#144167=CARTESIAN_POINT('Ctrl Pts',(16.3104425025438,-18.1273976373283,
1.00841709328394));
#144168=CARTESIAN_POINT('Ctrl Pts',(16.3297568808632,-18.0706314812951,
1.01141354667312));
#144169=CARTESIAN_POINT('Ctrl Pts',(16.3510510092264,-18.0145893008769,
1.0144100000623));
#144170=CARTESIAN_POINT('Ctrl Pts',(16.3742656062904,-17.9594005887852,
1.01740645345148));
#144171=CARTESIAN_POINT('Ctrl Pts',(16.4066870283893,-17.8823242335553,
1.02159128939168));
#144172=CARTESIAN_POINT('Ctrl Pts',(16.442949046845,-17.806694695872,1.02577612533188));
#144173=CARTESIAN_POINT('Ctrl Pts',(16.4829010339938,-17.7329210668517,
1.02996096127207));
#144174=CARTESIAN_POINT('Ctrl Pts',(16.5227961707087,-17.6592524154088,
1.03413984232102));
#144175=CARTESIAN_POINT('Ctrl Pts',(16.5663706293486,-17.5874348279767,
1.03831872336996));
#144176=CARTESIAN_POINT('Ctrl Pts',(16.6134257549123,-17.517857443951,1.0424976044189));
#144177=CARTESIAN_POINT('Ctrl Pts',(16.6613214140263,-17.4470372170912,
1.04675113174031));
#144178=CARTESIAN_POINT('Ctrl Pts',(16.7128231258243,-17.378538458199,1.05100465906173));
#144179=CARTESIAN_POINT('Ctrl Pts',(16.767672421654,-17.312745335637,1.05525818638315));
#144180=CARTESIAN_POINT('Ctrl Pts',(16.8214616389431,-17.2482238041918,
1.05942950530122));
#144181=CARTESIAN_POINT('Ctrl Pts',(16.8784698848833,-17.1863046245575,
1.06360082421929));
#144182=CARTESIAN_POINT('Ctrl Pts',(16.9384107688485,-17.1273193942576,
1.06777214313735));
#144183=CARTESIAN_POINT('Ctrl Pts',(16.9983315441488,-17.0683539520246,
1.07194206268243));
#144184=CARTESIAN_POINT('Ctrl Pts',(17.0611826759855,-17.0123208267143,
1.07611198222751));
#144185=CARTESIAN_POINT('Ctrl Pts',(17.1266402234641,-16.9595154834292,
1.08028190177259));
#144186=CARTESIAN_POINT('Ctrl Pts',(17.192095441962,-16.9067120189591,1.08445167295186));
#144187=CARTESIAN_POINT('Ctrl Pts',(17.2601565331721,-16.8571363963205,
1.08862144413112));
#144188=CARTESIAN_POINT('Ctrl Pts',(17.3304667893585,-16.8110435486385,
1.09279121531039));
#144189=CARTESIAN_POINT('Ctrl Pts',(17.4032413988251,-16.7633351605427,
1.09710713571227));
#144190=CARTESIAN_POINT('Ctrl Pts',(17.4784253279814,-16.7193585145734,
1.10142305611414));
#144191=CARTESIAN_POINT('Ctrl Pts',(17.5555924665286,-16.6793461141085,
1.10573897651602));
#144192=CARTESIAN_POINT('Ctrl Pts',(17.6302537175966,-16.6406330565404,
1.10991474385404));
#144193=CARTESIAN_POINT('Ctrl Pts',(17.7067708977367,-16.6056308716597,
1.11409051119206));
#144194=CARTESIAN_POINT('Ctrl Pts',(17.7847367550312,-16.5745014633546,
1.11826627853008));
#144195=CARTESIAN_POINT('Ctrl Pts',(17.8666278144112,-16.5418048405963,
1.12265227546389));
#144196=CARTESIAN_POINT('Ctrl Pts',(17.950116694982,-16.5133813683478,1.12703827239769));
#144197=CARTESIAN_POINT('Ctrl Pts',(18.0347145687176,-16.4893591643124,
1.13142426933149));
#144198=CARTESIAN_POINT('Ctrl Pts',(18.1193124424532,-16.465336960277,1.1358102662653));
#144199=CARTESIAN_POINT('Ctrl Pts',(18.2050187273114,-16.445716079792,1.1401962631991));
#144200=CARTESIAN_POINT('Ctrl Pts',(18.2913357970735,-16.4305622348653,
1.14458226013291));
#144201=CARTESIAN_POINT('Ctrl Pts',(18.3736918330588,-16.4161037899536,
1.14876698654111));
#144202=CARTESIAN_POINT('Ctrl Pts',(18.4569101597461,-16.4056576064885,
1.1529517129493));
#144203=CARTESIAN_POINT('Ctrl Pts',(18.5405652843443,-16.3993184666357,
1.1571364393575));
#144204=CARTESIAN_POINT('Ctrl Pts',(18.6241013829374,-16.3929883462242,
1.16131521166224));
#144205=CARTESIAN_POINT('Ctrl Pts',(18.7080725902024,-16.3907536966889,
1.16549398396698));
#144206=CARTESIAN_POINT('Ctrl Pts',(18.7920441924572,-16.3926581174603,
1.16967275627172));
#144207=CARTESIAN_POINT('Ctrl Pts',(18.8775185302511,-16.3945966192864,
1.17392631087766));
#144208=CARTESIAN_POINT('Ctrl Pts',(18.9629928024743,-16.4008238793069,
1.1781798654836));
#144209=CARTESIAN_POINT('Ctrl Pts',(19.0480040551094,-16.4113305107955,
1.18243342008954));
#144210=CARTESIAN_POINT('Ctrl Pts',(19.1313696330155,-16.421633751587,1.18660463303945));
#144211=CARTESIAN_POINT('Ctrl Pts',(19.2142894806513,-16.4360520981611,
1.19077584598936));
#144212=CARTESIAN_POINT('Ctrl Pts',(19.2963297776568,-16.4545242301154,
1.19494705893927));
#144213=CARTESIAN_POINT('Ctrl Pts',(19.3783425766114,-16.4729901706292,
1.199116873793));
#144214=CARTESIAN_POINT('Ctrl Pts',(19.4594759620237,-16.4955070970836,
1.20328668864672));
#144215=CARTESIAN_POINT('Ctrl Pts',(19.5393061703828,-16.5219625575018,
1.20745650350045));
#144216=CARTESIAN_POINT('Ctrl Pts',(19.6191335655528,-16.5484170856385,
1.21162617141134));
#144217=CARTESIAN_POINT('Ctrl Pts',(19.6976574385902,-16.5788097262656,
1.21579583932222));
#144218=CARTESIAN_POINT('Ctrl Pts',(19.7744703716763,-16.6129785367244,
1.2199655072331));
#144219=CARTESIAN_POINT('Ctrl Pts',(19.853979869365,-16.6483468639975,1.22428155386487));
#144220=CARTESIAN_POINT('Ctrl Pts',(19.9316555820171,-16.6877612115752,
1.22859760049664));
#144221=CARTESIAN_POINT('Ctrl Pts',(20.0070713209912,-16.7309891014068,
1.23291364712841));
#144222=CARTESIAN_POINT('Ctrl Pts',(20.080034189258,-16.772811019141,1.23708931584307));
#144223=CARTESIAN_POINT('Ctrl Pts',(20.1508814689922,-16.8182019195625,
1.24126498455773));
#144224=CARTESIAN_POINT('Ctrl Pts',(20.2192566105122,-16.866907004249,1.24544065327239));
#144225=CARTESIAN_POINT('Ctrl Pts',(20.2910797123248,-16.9180681452494,
1.24982688886272));
#144226=CARTESIAN_POINT('Ctrl Pts',(20.3601743388774,-16.9728861439699,
1.25421312445304));
#144227=CARTESIAN_POINT('Ctrl Pts',(20.4261681146539,-17.0310192422232,
1.25859936004337));
#144228=CARTESIAN_POINT('Ctrl Pts',(20.4921618904303,-17.0891523404765,
1.26298559563369));
#144229=CARTESIAN_POINT('Ctrl Pts',(20.5550544537331,-17.1506000785723,
1.26737183122402));
#144230=CARTESIAN_POINT('Ctrl Pts',(20.614521157858,-17.2149795122542,1.27175806681434));
#144231=CARTESIAN_POINT('Ctrl Pts',(20.6712532028065,-17.2763983680518,
1.2759425952547));
#144232=CARTESIAN_POINT('Ctrl Pts',(20.7250787526129,-17.3407138524111,
1.28012712369507));
#144233=CARTESIAN_POINT('Ctrl Pts',(20.7756877943714,-17.4076195577789,
1.28431165213543));
#144234=CARTESIAN_POINT('Ctrl Pts',(20.8262247790096,-17.4744300028477,
1.28849022264697));
#144235=CARTESIAN_POINT('Ctrl Pts',(20.873554077068,-17.5438229797257,1.29266879315851));
#144236=CARTESIAN_POINT('Ctrl Pts',(20.9174037166616,-17.6154566187107,
1.29684736367005));
#144237=CARTESIAN_POINT('Ctrl Pts',(20.9620407587122,-17.6883765739312,
1.30110096824612));
#144238=CARTESIAN_POINT('Ctrl Pts',(21.0030716111862,-17.7636181037575,
1.30535457282219));
#144239=CARTESIAN_POINT('Ctrl Pts',(21.04025352208,-17.8407868377788,1.30960817739826));
#144240=CARTESIAN_POINT('Ctrl Pts',(21.0767133920066,-17.9164570208649,
1.3137791806048));
#144241=CARTESIAN_POINT('Ctrl Pts',(21.1094722614084,-17.9939797943654,
1.31795018381133));
#144242=CARTESIAN_POINT('Ctrl Pts',(21.1383468600458,-18.0729572384759,
1.32212118701786));
#144243=CARTESIAN_POINT('Ctrl Pts',(21.1672117626761,-18.1519081621879,
1.32629078961353));
#144244=CARTESIAN_POINT('Ctrl Pts',(21.1921948271095,-18.2323123546667,
1.33046039220919));
#144245=CARTESIAN_POINT('Ctrl Pts',(21.2131612187129,-18.3137526720542,
1.33462999480485));
#144246=CARTESIAN_POINT('Ctrl Pts',(21.2341268601602,-18.3951900755901,
1.33879944821638));
#144247=CARTESIAN_POINT('Ctrl Pts',(21.2510760006384,-18.4776630845828,
1.34296890162792));
#144248=CARTESIAN_POINT('Ctrl Pts',(21.263924266104,-18.560741507724,1.34713835503945));
#144249=CARTESIAN_POINT('Ctrl Pts',(21.2772250217302,-18.6467457864309,
1.35145464824414));
#144250=CARTESIAN_POINT('Ctrl Pts',(21.2861305792208,-18.7333983970714,
1.35577094144884));
#144251=CARTESIAN_POINT('Ctrl Pts',(21.2906057031231,-18.8202150283277,
1.36008723465353));
#144252=CARTESIAN_POINT('Ctrl Pts',(21.2949348018955,-18.90419879727,1.36426268543923));
#144253=CARTESIAN_POINT('Ctrl Pts',(21.2951181997827,-18.9883355761622,
1.36843813622492));
#144254=CARTESIAN_POINT('Ctrl Pts',(21.2911771392428,-19.0721876804587,
1.37261358701061));
#144255=CARTESIAN_POINT('Ctrl Pts',(21.2870366744248,-19.1602824164424,
1.3770003014248));
#144256=CARTESIAN_POINT('Ctrl Pts',(21.2783434340466,-19.2480623296263,
1.381387015839));
#144257=CARTESIAN_POINT('Ctrl Pts',(21.2651832590201,-19.3350291232486,
1.38577373025319));
#144258=CARTESIAN_POINT('Ctrl Pts',(21.2520230839935,-19.421995916871,1.39016044466739));
#144259=CARTESIAN_POINT('Ctrl Pts',(21.2343961652463,-19.5081490374756,
1.39454715908158));
#144260=CARTESIAN_POINT('Ctrl Pts',(21.2124488480671,-19.5930080401328,
1.39893387349578));
#144261=CARTESIAN_POINT('Ctrl Pts',(21.1915163486012,-19.6739432639369,
1.40311775147879));
#144262=CARTESIAN_POINT('Ctrl Pts',(21.1665762580736,-19.7540026330353,
1.40730162946179));
#144263=CARTESIAN_POINT('Ctrl Pts',(21.1377183899587,-19.8327598434161,
1.4114855074448));
#144264=CARTESIAN_POINT('Ctrl Pts',(21.1088989075933,-19.9114122936482,
1.41566382017635));
#144265=CARTESIAN_POINT('Ctrl Pts',(21.0761721509734,-19.988765596162,1.4198421329079));
#144266=CARTESIAN_POINT('Ctrl Pts',(21.0396783452697,-20.0644061165575,
1.42402044563945));
#144267=CARTESIAN_POINT('Ctrl Pts',(21.0032221304776,-20.1399687224669,
1.4281944544465));
#144268=CARTESIAN_POINT('Ctrl Pts',(20.9630067721328,-20.2138216382969,
1.43236846325355));
#144269=CARTESIAN_POINT('Ctrl Pts',(20.9192209903055,-20.285570104467,1.4365424720606));
#144270=CARTESIAN_POINT('Ctrl Pts',(20.8754640550467,-20.3572713019358,
1.44071373098342));
#144271=CARTESIAN_POINT('Ctrl Pts',(20.8281416060815,-20.4268704111564,
1.44488498990625));
#144272=CARTESIAN_POINT('Ctrl Pts',(20.7774882140691,-20.4939973796867,
1.44905624882907));
#144273=CARTESIAN_POINT('Ctrl Pts',(20.7268554189014,-20.5610970528337,
1.45322581162121));
#144274=CARTESIAN_POINT('Ctrl Pts',(20.6728946507595,-20.6257262172986,
1.45739537441335));
#144275=CARTESIAN_POINT('Ctrl Pts',(20.6158828807294,-20.6875451083788,
1.46156493720549));
#144276=CARTESIAN_POINT('Ctrl Pts',(20.5588584185249,-20.7493777618128,
1.46573542824136));
#144277=CARTESIAN_POINT('Ctrl Pts',(20.4987819053236,-20.8083985496803,
1.46990591927723));
#144278=CARTESIAN_POINT('Ctrl Pts',(20.4359689278453,-20.8643027398006,
1.47407641031309));
#144279=CARTESIAN_POINT('Ctrl Pts',(20.3899160356864,-20.9052902831747,
1.47713410924149));
#144280=CARTESIAN_POINT('Ctrl Pts',(20.3423929948226,-20.9446032322061,
1.48019180816988));
#144281=CARTESIAN_POINT('Ctrl Pts',(20.2935357468249,-20.9821350335323,
1.48324950709828));
#144282=CARTESIAN_POINT('Origin',(18.734,-18.952,-1.76670989022851));
#144283=CARTESIAN_POINT('',(20.2935357468249,-20.9821350335323,2.34989189284213));
#144284=CARTESIAN_POINT('',(20.2935357468249,-20.9821350335323,2.28327545627391));
#144285=CARTESIAN_POINT('',(20.2935357468249,-20.9821350335323,-1.76670989022851));
#144286=CARTESIAN_POINT('',(16.1742339454204,-18.95300766776,1.83329006740176));
#144287=CARTESIAN_POINT('Ctrl Pts',(16.174000198019,-18.953006904815,1.8332901097715));
#144288=CARTESIAN_POINT('Ctrl Pts',(16.1739663681252,-18.8669962708809,
1.83754657623655));
#144289=CARTESIAN_POINT('Ctrl Pts',(16.1782715498346,-18.7810104795588,
1.8418030427016));
#144290=CARTESIAN_POINT('Ctrl Pts',(16.186881959491,-18.6955049947587,1.84605950916664));
#144291=CARTESIAN_POINT('Ctrl Pts',(16.1954973714571,-18.6099498346313,
1.85031844847147));
#144292=CARTESIAN_POINT('Ctrl Pts',(16.2084229438518,-18.5248759665389,
1.85457738777631));
#144293=CARTESIAN_POINT('Ctrl Pts',(16.2255732751413,-18.4407316105854,
1.85883632708114));
#144294=CARTESIAN_POINT('Ctrl Pts',(16.242752034236,-18.3564477798121,1.86310232585877));
#144295=CARTESIAN_POINT('Ctrl Pts',(16.2641694501873,-18.273096962922,1.86736832463641));
#144296=CARTESIAN_POINT('Ctrl Pts',(16.2896893999554,-18.1911151923519,
1.87163432341404));
#144297=CARTESIAN_POINT('Ctrl Pts',(16.315231796287,-18.1090613131363,1.87590407443307));
#144298=CARTESIAN_POINT('Ctrl Pts',(16.3448837660304,-18.02837928517,1.88017382545211));
#144299=CARTESIAN_POINT('Ctrl Pts',(16.3784607475836,-17.9494857455749,
1.88444357647114));
#144300=CARTESIAN_POINT('Ctrl Pts',(16.4121081360754,-17.8704267756062,
1.88872228065047));
#144301=CARTESIAN_POINT('Ctrl Pts',(16.4496967908486,-17.7931641763823,
1.89300098482979));
#144302=CARTESIAN_POINT('Ctrl Pts',(16.4909957508862,-17.7180907900264,
1.89727968900912));
#144303=CARTESIAN_POINT('Ctrl Pts',(16.5197685295266,-17.6657875377064,
1.90026064078387));
#144304=CARTESIAN_POINT('Ctrl Pts',(16.550341278611,-17.6145463427439,1.90324159255863));
#144305=CARTESIAN_POINT('Ctrl Pts',(16.582623920045,-17.5644910945881,1.90622254433338));
#144306=CARTESIAN_POINT('Ctrl Pts',(16.6279420233621,-17.494223953898,1.91040717962067));
#144307=CARTESIAN_POINT('Ctrl Pts',(16.6767906254559,-17.4260486191802,
1.91459181490796));
#144308=CARTESIAN_POINT('Ctrl Pts',(16.7289503547201,-17.3603417703656,
1.91877645019526));
#144309=CARTESIAN_POINT('Ctrl Pts',(16.7810358412115,-17.2947284469338,
1.92295512918386));
#144310=CARTESIAN_POINT('Ctrl Pts',(16.8364228098559,-17.2315769875612,
1.92713380817247));
#144311=CARTESIAN_POINT('Ctrl Pts',(16.8948480567242,-17.1712360825912,
1.93131248716107));
#144312=CARTESIAN_POINT('Ctrl Pts',(16.9543205181338,-17.1098136268106,
1.93556606482165));
#144313=CARTESIAN_POINT('Ctrl Pts',(17.0169409883808,-17.0513038784722,
1.93981964248222));
#144314=CARTESIAN_POINT('Ctrl Pts',(17.0823881640358,-16.9960403012069,
1.94407322014279));
#144315=CARTESIAN_POINT('Ctrl Pts',(17.1465665360848,-16.9418481013602,
1.94824433504435));
#144316=CARTESIAN_POINT('Ctrl Pts',(17.2134626230333,-16.8907776412553,
1.95241544994592));
#144317=CARTESIAN_POINT('Ctrl Pts',(17.2827368115807,-16.8431057025211,
1.95658656484748));
#144318=CARTESIAN_POINT('Ctrl Pts',(17.3519877545941,-16.795449760505,1.96075628009652));
#144319=CARTESIAN_POINT('Ctrl Pts',(17.4236148357283,-16.7511903355778,
1.96492599534557));
#144320=CARTESIAN_POINT('Ctrl Pts',(17.4972477392743,-16.7105621031155,
1.96909571059461));
#144321=CARTESIAN_POINT('Ctrl Pts',(17.570878022714,-16.6699353163424,1.97326527747115));
#144322=CARTESIAN_POINT('Ctrl Pts',(17.6465135834573,-16.63293968663,1.9774348443477));
#144323=CARTESIAN_POINT('Ctrl Pts',(17.7237588789708,-16.599764281076,1.98160441122425));
#144324=CARTESIAN_POINT('Ctrl Pts',(17.8037199857115,-16.5654224855398,
1.98592057287346));
#144325=CARTESIAN_POINT('Ctrl Pts',(17.8854056436378,-16.5351747548241,
1.99023673452268));
#144326=CARTESIAN_POINT('Ctrl Pts',(17.9683557183505,-16.5091760534215,
1.99455289617189));
#144327=CARTESIAN_POINT('Ctrl Pts',(18.0486037412862,-16.4840242450153,
1.9987284612961));
#144328=CARTESIAN_POINT('Ctrl Pts',(18.1300346026626,-16.4628489694374,
2.0029040264203));
#144329=CARTESIAN_POINT('Ctrl Pts',(18.2122191473171,-16.4457388919401,
2.0070795915445));
#144330=CARTESIAN_POINT('Ctrl Pts',(18.2985545773168,-16.4277646377265,
2.01146605145622));
#144331=CARTESIAN_POINT('Ctrl Pts',(18.3857212504154,-16.414277123386,2.01585251136794));
#144332=CARTESIAN_POINT('Ctrl Pts',(18.4732153214913,-16.4053175793878,
2.02023897127966));
#144333=CARTESIAN_POINT('Ctrl Pts',(18.5607093925672,-16.3963580353896,
2.02462543119138));
#144334=CARTESIAN_POINT('Ctrl Pts',(18.6485302783096,-16.3919264150074,
2.0290118911031));
#144335=CARTESIAN_POINT('Ctrl Pts',(18.7361763184416,-16.3920009250709,
2.03339835101482));
#144336=CARTESIAN_POINT('Ctrl Pts',(18.8197896747137,-16.3920720068501,
2.03758298542408));
#144337=CARTESIAN_POINT('Ctrl Pts',(18.9035551457573,-16.3962439324391,
2.04176761983334));
#144338=CARTESIAN_POINT('Ctrl Pts',(18.9870372618429,-16.4045361348747,
2.0459522542426));
#144339=CARTESIAN_POINT('Ctrl Pts',(19.0704005515259,-16.4128165343922,
2.05013093234557));
#144340=CARTESIAN_POINT('Ctrl Pts',(19.1534808335077,-16.4252055165322,
2.05430961044854));
#144341=CARTESIAN_POINT('Ctrl Pts',(19.2358424472477,-16.4416705080527,
2.05848828855151));
#144342=CARTESIAN_POINT('Ctrl Pts',(19.3196803332532,-16.4584306226193,
2.06274186643254));
#144343=CARTESIAN_POINT('Ctrl Pts',(19.4027730512138,-16.4794143083236,
2.06699544431357));
#144344=CARTESIAN_POINT('Ctrl Pts',(19.4846662953171,-16.5045318974346,
2.0712490221946));
#144345=CARTESIAN_POINT('Ctrl Pts',(19.5649718796635,-16.5291625332462,
2.07542013619845));
#144346=CARTESIAN_POINT('Ctrl Pts',(19.6441236233212,-16.5577680742246,
2.07959125020228));
#144347=CARTESIAN_POINT('Ctrl Pts',(19.721704970629,-16.5902127760963,2.08376236420613));
#144348=CARTESIAN_POINT('Ctrl Pts',(19.7992602848132,-16.6226465908545,
2.0879320785549));
#144349=CARTESIAN_POINT('Ctrl Pts',(19.8752458251392,-16.6589168306477,
2.09210179290367));
#144350=CARTESIAN_POINT('Ctrl Pts',(19.949263822001,-16.6988391440167,2.09627150725245));
#144351=CARTESIAN_POINT('Ctrl Pts',(20.0232791850289,-16.7387600368021,
2.10044107322737));
#144352=CARTESIAN_POINT('Ctrl Pts',(20.0953267393063,-16.7823325256475,
2.1046106392023));
#144353=CARTESIAN_POINT('Ctrl Pts',(20.1650334097648,-16.8293263604273,
2.10878020517723));
#144354=CARTESIAN_POINT('Ctrl Pts',(20.2371908797447,-16.8779724397775,
2.11309636788714));
#144355=CARTESIAN_POINT('Ctrl Pts',(20.30683935496,-16.9302846355633,2.11741253059706));
#144356=CARTESIAN_POINT('Ctrl Pts',(20.3735994723764,-16.9859599266081,
2.12172869330698));
#144357=CARTESIAN_POINT('Ctrl Pts',(20.4381848869935,-17.03982160174,2.12590425753548));
#144358=CARTESIAN_POINT('Ctrl Pts',(20.5000669160013,-17.0968302774532,
2.13007982176398));
#144359=CARTESIAN_POINT('Ctrl Pts',(20.5589387125302,-17.1566730950859,
2.13425538599248));
#144360=CARTESIAN_POINT('Ctrl Pts',(20.6207839821291,-17.2195384297327,
2.13864184794311));
#144361=CARTESIAN_POINT('Ctrl Pts',(20.6793065465875,-17.2855312985542,
2.14302830989374));
#144362=CARTESIAN_POINT('Ctrl Pts',(20.7341990153404,-17.354250364096,2.14741477184436));
#144363=CARTESIAN_POINT('Ctrl Pts',(20.7890914840933,-17.4229694296379,
2.15180123379499));
#144364=CARTESIAN_POINT('Ctrl Pts',(20.840353580694,-17.4944141761338,2.15618769574562));
#144365=CARTESIAN_POINT('Ctrl Pts',(20.8877320902557,-17.5681509896658,
2.16057415769624));
#144366=CARTESIAN_POINT('Ctrl Pts',(20.9329306422981,-17.638495059893,2.16475879183927));
#144367=CARTESIAN_POINT('Ctrl Pts',(20.9747633711847,-17.7111867434279,
2.16894342598229));
#144368=CARTESIAN_POINT('Ctrl Pts',(21.0129782252709,-17.7858703979656,
2.17312806012532));
#144369=CARTESIAN_POINT('Ctrl Pts',(21.0511386851992,-17.8604477494804,
2.17730673795485));
#144370=CARTESIAN_POINT('Ctrl Pts',(21.0856912912936,-17.9370110341171,
2.18148541578439));
#144371=CARTESIAN_POINT('Ctrl Pts',(21.116427617672,-18.0151762991077,2.18566409361392));
#144372=CARTESIAN_POINT('Ctrl Pts',(21.1477148729796,-18.0947426263206,
2.18991767156241));
#144373=CARTESIAN_POINT('Ctrl Pts',(21.1750474280233,-18.1759685243987,
2.1941712495109));
#144374=CARTESIAN_POINT('Ctrl Pts',(21.1982547719715,-18.2584234585746,
2.19842482745939));
#144375=CARTESIAN_POINT('Ctrl Pts',(21.2210121944976,-18.33927983665,2.20259594117397));
#144376=CARTESIAN_POINT('Ctrl Pts',(21.2398027993344,-18.421317558152,2.20676705488855));
#144377=CARTESIAN_POINT('Ctrl Pts',(21.2545152522161,-18.504112889953,2.21093816860314));
#144378=CARTESIAN_POINT('Ctrl Pts',(21.269222768182,-18.5868804389239,2.21510788265736));
#144379=CARTESIAN_POINT('Ctrl Pts',(21.2798547695695,-18.6704046407403,
2.21927759671159));
#144380=CARTESIAN_POINT('Ctrl Pts',(21.2863509615978,-18.7542512482193,
2.22344731076582));
#144381=CARTESIAN_POINT('Ctrl Pts',(21.2928469224598,-18.838094872027,2.22761687644128));
#144382=CARTESIAN_POINT('Ctrl Pts',(21.2952073318929,-18.9222604199623,
2.23178644211675));
#144383=CARTESIAN_POINT('Ctrl Pts',(21.2934238553148,-19.0063095649563,
2.23595600779222));
#144384=CARTESIAN_POINT('Ctrl Pts',(21.2915776736488,-19.0933137860529,
2.240272170841));
#144385=CARTESIAN_POINT('Ctrl Pts',(21.2852907961481,-19.1801927391156,
2.24458833388979));
#144386=CARTESIAN_POINT('Ctrl Pts',(21.2746126736341,-19.2664634200821,
2.24890449693858));
#144387=CARTESIAN_POINT('Ctrl Pts',(21.2642823912523,-19.3499238312635,
2.25308006085835));
#144388=CARTESIAN_POINT('Ctrl Pts',(21.2498426885289,-19.432814534908,2.25725562477812));
#144389=CARTESIAN_POINT('Ctrl Pts',(21.2313905396644,-19.5147081769395,
2.26143118869789));
#144390=CARTESIAN_POINT('Ctrl Pts',(21.2120064127096,-19.6007380895309,
2.26581765131119));
#144391=CARTESIAN_POINT('Ctrl Pts',(21.1881940056837,-19.6856670076436,
2.27020411392449));
#144392=CARTESIAN_POINT('Ctrl Pts',(21.1601243952761,-19.7690192278315,
2.27459057653779));
#144393=CARTESIAN_POINT('Ctrl Pts',(21.1320547848684,-19.8523714480194,
2.27897703915109));
#144394=CARTESIAN_POINT('Ctrl Pts',(21.0997282551217,-19.9341464586594,
2.28336350176438));
#144395=CARTESIAN_POINT('Ctrl Pts',(21.0633723464422,-20.0138966388639,
2.28774996437768));
#144396=CARTESIAN_POINT('Ctrl Pts',(21.028688700058,-20.0899785509864,2.29193466292279));
#144397=CARTESIAN_POINT('Ctrl Pts',(20.9902091092465,-20.1645010086708,
2.2961193614679));
#144398=CARTESIAN_POINT('Ctrl Pts',(20.9480961900739,-20.2370595554683,
2.30030406001301));
#144399=CARTESIAN_POINT('Ctrl Pts',(20.9060523787106,-20.3094990328135,
2.30448189141722));
#144400=CARTESIAN_POINT('Ctrl Pts',(20.8603873210434,-20.3799806118459,
2.30865972282143));
#144401=CARTESIAN_POINT('Ctrl Pts',(20.811310912052,-20.4481214438239,2.31283755422565));
#144402=CARTESIAN_POINT('Ctrl Pts',(20.7622817553052,-20.5161966677566,
2.31701136308795));
#144403=CARTESIAN_POINT('Ctrl Pts',(20.7098480348053,-20.5819352475709,
2.32118517195026));
#144404=CARTESIAN_POINT('Ctrl Pts',(20.6542641570203,-20.6449812660698,
2.32535898081256));
#144405=CARTESIAN_POINT('Ctrl Pts',(20.5987134202835,-20.7079896943315,
2.32953030110432));
#144406=CARTESIAN_POINT('Ctrl Pts',(20.5400165562304,-20.7683084024141,
2.33370162139608));
#144407=CARTESIAN_POINT('Ctrl Pts',(20.4784688818988,-20.825613706207,2.33787294168784));
#144408=CARTESIAN_POINT('Ctrl Pts',(20.4193558241849,-20.8806522071286,
2.34187925873927));
#144409=CARTESIAN_POINT('Ctrl Pts',(20.3576135312872,-20.9329109209508,
2.3458855757907));
#144410=CARTESIAN_POINT('Ctrl Pts',(20.2935357468249,-20.9821350335323,
2.34989189284213));
#144411=CARTESIAN_POINT('Ctrl Pts',(20.294072348973,-20.9828452881321,1.55000082941897));
#144412=CARTESIAN_POINT('Ctrl Pts',(19.7490823179128,-21.3927990376574,
1.58395752993615));
#144413=CARTESIAN_POINT('Ctrl Pts',(18.1401763549456,-21.8312444115751,
1.6603061660138));
#144414=CARTESIAN_POINT('Ctrl Pts',(16.4202753042621,-20.536339124494,1.75473569408312));
#144415=CARTESIAN_POINT('Ctrl Pts',(16.1765569610219,-19.3178333678849,
1.81520852163526));
#144416=CARTESIAN_POINT('Ctrl Pts',(16.1778407221624,-18.9530194401788,
1.83328941362691));
#144417=CARTESIAN_POINT('',(16.1740004726294,-18.9504444093098,1.76670989019937));
#144418=CARTESIAN_POINT('Ctrl Pts',(20.2935357468249,-20.9821350335323,
1.48324950709828));
#144419=CARTESIAN_POINT('Ctrl Pts',(20.2268277705136,-21.0333796413724,
1.48742438218933));
#144420=CARTESIAN_POINT('Ctrl Pts',(20.1576316687033,-21.0813019538135,
1.49159925728038));
#144421=CARTESIAN_POINT('Ctrl Pts',(20.0863185925296,-21.1256684255651,
1.49577413237143));
#144422=CARTESIAN_POINT('Ctrl Pts',(20.0149603823384,-21.170062976839,1.49995164973925));
#144423=CARTESIAN_POINT('Ctrl Pts',(19.9414829328826,-21.2108969849863,
1.50412916710708));
#144424=CARTESIAN_POINT('Ctrl Pts',(19.8662815900183,-21.2479831011803,
1.50830668447491));
#144425=CARTESIAN_POINT('Ctrl Pts',(19.7909572329255,-21.28512988278,1.51249103541853));
#144426=CARTESIAN_POINT('Ctrl Pts',(19.7139037757318,-21.3185163539148,
1.51667538636215));
#144427=CARTESIAN_POINT('Ctrl Pts',(19.6355356527249,-21.3480036450026,
1.52085973730577));
#144428=CARTESIAN_POINT('Ctrl Pts',(19.6027605043788,-21.3603358319002,
1.52260971826292));
#144429=CARTESIAN_POINT('Ctrl Pts',(19.569755577939,-21.3719866256104,1.52435969922007));
#144430=CARTESIAN_POINT('Ctrl Pts',(19.5365517913642,-21.3829485025763,
1.52610968017722));
#144431=CARTESIAN_POINT('Ctrl Pts',(19.4571532093435,-21.4091610999082,
1.53029432358371));
#144432=CARTESIAN_POINT('Ctrl Pts',(19.376321311697,-21.4315284613918,1.53447896699021));
#144433=CARTESIAN_POINT('Ctrl Pts',(19.294463394386,-21.4498952707336,1.53866361039671));
#144434=CARTESIAN_POINT('Ctrl Pts',(19.2127219863795,-21.4682359383869,
1.54284229775267));
#144435=CARTESIAN_POINT('Ctrl Pts',(19.1299579044461,-21.4825872641847,
1.54702098510862));
#144436=CARTESIAN_POINT('Ctrl Pts',(19.0465949711256,-21.4928432427104,
1.55119967246457));
#144437=CARTESIAN_POINT('Ctrl Pts',(18.9617380510235,-21.5032830235057,
1.55545324806433));
#144438=CARTESIAN_POINT('Ctrl Pts',(18.8762610608014,-21.5094790670078,
1.55970682366408));
#144439=CARTESIAN_POINT('Ctrl Pts',(18.7906234643,-21.5113737091896,1.56396039926383));
#144440=CARTESIAN_POINT('Ctrl Pts',(18.7066458764304,-21.5132316254179,
1.56813152308422));
#144441=CARTESIAN_POINT('Ctrl Pts',(18.6225143342412,-21.5109533994767,
1.5723026469046));
#144442=CARTESIAN_POINT('Ctrl Pts',(18.5386669500421,-21.5045369732081,
1.57647377072499));
#144443=CARTESIAN_POINT('Ctrl Pts',(18.4548476977165,-21.4981226997328,
1.5806434950798));
#144444=CARTESIAN_POINT('Ctrl Pts',(18.3713128723448,-21.4875730184253,
1.58481321943461));
#144445=CARTESIAN_POINT('Ctrl Pts',(18.2884980293892,-21.4729379195414,
1.58898294378941));
#144446=CARTESIAN_POINT('Ctrl Pts',(18.2056861297709,-21.4583033408063,
1.59315251994729));
#144447=CARTESIAN_POINT('Ctrl Pts',(18.1235946145539,-21.4395837140867,
1.59732209610518));
#144448=CARTESIAN_POINT('Ctrl Pts',(18.0426500220353,-21.4168803638246,
1.60149167226306));
#144449=CARTESIAN_POINT('Ctrl Pts',(17.9588599464441,-21.3933789120853,
1.60580782347935));
#144450=CARTESIAN_POINT('Ctrl Pts',(17.8762994409707,-21.3656085753716,
1.61012397469565));
#144451=CARTESIAN_POINT('Ctrl Pts',(17.7954238784078,-21.3337377823717,
1.61444012591195));
#144452=CARTESIAN_POINT('Ctrl Pts',(17.7171824220401,-21.3029050168134,
1.61861570066365));
#144453=CARTESIAN_POINT('Ctrl Pts',(17.6405182464777,-21.2682350343783,
1.62279127541534));
#144454=CARTESIAN_POINT('Ctrl Pts',(17.5658209821028,-21.2299283970627,
1.62696685016703));
#144455=CARTESIAN_POINT('Ctrl Pts',(17.4873515385791,-21.1896872913332,
1.63135328961563));
#144456=CARTESIAN_POINT('Ctrl Pts',(17.4110533971718,-21.1454328556654,
1.63573972906424));
#144457=CARTESIAN_POINT('Ctrl Pts',(17.3373445042313,-21.097449469491,1.64012616851284));
#144458=CARTESIAN_POINT('Ctrl Pts',(17.2636356112909,-21.0494660833166,
1.64451260796144));
#144459=CARTESIAN_POINT('Ctrl Pts',(17.1925163913427,-20.9977541493591,
1.64889904741004));
#144460=CARTESIAN_POINT('Ctrl Pts',(17.1243635064003,-20.9426457139511,
1.65328548685865));
#144461=CARTESIAN_POINT('Ctrl Pts',(17.0601943718463,-20.8907585398463,
1.6574155251311));
#144462=CARTESIAN_POINT('Ctrl Pts',(16.9984022164044,-20.8356563912925,
1.66154556340355));
#144463=CARTESIAN_POINT('Ctrl Pts',(16.9393333497915,-20.7775880188667,
1.66567560167601));
#144464=CARTESIAN_POINT('Ctrl Pts',(16.8791242536685,-20.7183987298625,
1.66988536369781));
#144465=CARTESIAN_POINT('Ctrl Pts',(16.8217451259872,-20.6561277338344,
1.67409512571962));
#144466=CARTESIAN_POINT('Ctrl Pts',(16.7675298313412,-20.5910836085371,
1.67830488774143));
#144467=CARTESIAN_POINT('Ctrl Pts',(16.7144792342514,-20.5274368146437,
1.6824242121926));
#144468=CARTESIAN_POINT('Ctrl Pts',(16.6644582227548,-20.4611352262018,
1.68654353664378));
#144469=CARTESIAN_POINT('Ctrl Pts',(16.6177431437369,-20.3925057855904,
1.69066286109495));
#144470=CARTESIAN_POINT('Ctrl Pts',(16.5710563620564,-20.3239179167901,
1.69477969029369));
#144471=CARTESIAN_POINT('Ctrl Pts',(16.5276718049372,-20.2530053838409,
1.69889651949243));
#144472=CARTESIAN_POINT('Ctrl Pts',(16.4878244177667,-20.1801267254559,
1.70301334869118));
#144473=CARTESIAN_POINT('Ctrl Pts',(16.4479884749074,-20.1072689980804,
1.70712899552195));
#144474=CARTESIAN_POINT('Ctrl Pts',(16.4116879114515,-20.0324466815215,
1.71124464235271));
#144475=CARTESIAN_POINT('Ctrl Pts',(16.3791125478311,-19.9560443653632,
1.71536028918348));
#144476=CARTESIAN_POINT('Ctrl Pts',(16.3452431871199,-19.8766071061112,
1.71963942260147));
#144477=CARTESIAN_POINT('Ctrl Pts',(16.3154014154543,-19.795462185038,1.72391855601946));
#144478=CARTESIAN_POINT('Ctrl Pts',(16.28974541526,-19.7130647311349,1.72819768943746));
#144479=CARTESIAN_POINT('Ctrl Pts',(16.2650470315947,-19.6337427825017,
1.73231710314623));
#144480=CARTESIAN_POINT('Ctrl Pts',(16.2442275676729,-19.5532606331567,
1.736436516855));
#144481=CARTESIAN_POINT('Ctrl Pts',(16.2273766226977,-19.4720377335941,
1.74055593056377));
#144482=CARTESIAN_POINT('Ctrl Pts',(16.2105163820987,-19.3907700283831,
1.74467761669822));
#144483=CARTESIAN_POINT('Ctrl Pts',(16.1976290876222,-19.3087612270287,
1.74879930283266));
#144484=CARTESIAN_POINT('Ctrl Pts',(16.1887526585032,-19.2264375531951,
1.7529209889671));
#144485=CARTESIAN_POINT('Ctrl Pts',(16.1798641546722,-19.1440018934889,
1.75704828188022));
#144486=CARTESIAN_POINT('Ctrl Pts',(16.1749974203025,-19.0612509779236,
1.76117557479333));
#144487=CARTESIAN_POINT('Ctrl Pts',(16.174138321227,-18.9786117558525,1.76530286770644));
#144488=CARTESIAN_POINT('Ctrl Pts',(16.1740406969692,-18.9692209964452,
1.76577187520409));
#144489=CARTESIAN_POINT('Ctrl Pts',(16.1739947684326,-18.9598316737892,
1.76624088270173));
#144490=CARTESIAN_POINT('Ctrl Pts',(16.1740004726294,-18.9504444093098,
1.76670989019937));
#144491=CARTESIAN_POINT('Ctrl Pts',(16.1740004726298,-18.9504444087268,
1.7667098902285));
#144492=CARTESIAN_POINT('Ctrl Pts',(16.1740562220874,-18.8586988534878,
1.77129369133236));
#144493=CARTESIAN_POINT('Ctrl Pts',(16.1790436176654,-18.7671041921699,
1.77587749243622));
#144494=CARTESIAN_POINT('Ctrl Pts',(16.1889163327552,-18.6760486877659,
1.78046129354008));
#144495=CARTESIAN_POINT('Ctrl Pts',(16.1979293239818,-18.5929223689306,
1.78464593360694));
#144496=CARTESIAN_POINT('Ctrl Pts',(16.2110359189735,-18.510083390536,1.78883057367379));
#144497=CARTESIAN_POINT('Ctrl Pts',(16.2282088655394,-18.4279668040492,
1.79301521374065));
#144498=CARTESIAN_POINT('Ctrl Pts',(16.24535736882,-18.3459670990266,1.79719389755824));
#144499=CARTESIAN_POINT('Ctrl Pts',(16.2665606337553,-18.2646881899744,
1.80137258137583));
#144500=CARTESIAN_POINT('Ctrl Pts',(16.2917396797569,-18.184559755964,1.80555126519342));
#144501=CARTESIAN_POINT('Ctrl Pts',(16.3173699983022,-18.1029952166205,
1.80980484165292));
#144502=CARTESIAN_POINT('Ctrl Pts',(16.3471199655449,-18.0226232777798,
1.81405841811242));
#144503=CARTESIAN_POINT('Ctrl Pts',(16.3808518405096,-17.9438860483621,
1.81831199457193));
#144504=CARTESIAN_POINT('Ctrl Pts',(16.4139298146452,-17.8666751598207,
1.82248311438838));
#144505=CARTESIAN_POINT('Ctrl Pts',(16.4508365039862,-17.7910366100589,
1.82665423420484));
#144506=CARTESIAN_POINT('Ctrl Pts',(16.4913923920135,-17.7173700487186,
1.8308253540213));
#144507=CARTESIAN_POINT('Ctrl Pts',(16.531934671396,-17.6437282064046,1.83499507420651));
#144508=CARTESIAN_POINT('Ctrl Pts',(16.5761234959118,-17.5720574410135,
1.83916479439172));
#144509=CARTESIAN_POINT('Ctrl Pts',(16.6237330298035,-17.5027335253662,
1.84333451457693));
#144510=CARTESIAN_POINT('Ctrl Pts',(16.6713408697582,-17.4334120762489,
1.8475040864044));
#144511=CARTESIAN_POINT('Ctrl Pts',(16.7223689159663,-17.3664376895872,
1.85167365823187));
#144512=CARTESIAN_POINT('Ctrl Pts',(16.7765483383152,-17.3021566764789,
1.85584323005933));
#144513=CARTESIAN_POINT('Ctrl Pts',(16.8326324736236,-17.2356158223938,
1.86015938590618));
#144514=CARTESIAN_POINT('Ctrl Pts',(16.8920933527671,-17.1719616497153,
1.86447554175303));
#144515=CARTESIAN_POINT('Ctrl Pts',(16.9545891225287,-17.1115389357183,
1.86879169759988));
#144516=CARTESIAN_POINT('Ctrl Pts',(17.0150492806953,-17.0530843097644,
1.87296726766114));
#144517=CARTESIAN_POINT('Ctrl Pts',(17.0783492743462,-16.9976541389962,
1.87714283772241));
#144518=CARTESIAN_POINT('Ctrl Pts',(17.1441452217407,-16.9455200514219,
1.88131840778368));
#144519=CARTESIAN_POINT('Ctrl Pts',(17.2132640597166,-16.8907530377263,
1.88570485652332));
#144520=CARTESIAN_POINT('Ctrl Pts',(17.2851371188669,-16.8396241343394,
1.89009130526296));
#144521=CARTESIAN_POINT('Ctrl Pts',(17.3593324936003,-16.792396043982,1.89447775400259));
#144522=CARTESIAN_POINT('Ctrl Pts',(17.4335278683337,-16.7451679536245,
1.89886420274223));
#144523=CARTESIAN_POINT('Ctrl Pts',(17.5100450162907,-16.7018408959928,
1.90325065148187));
#144524=CARTESIAN_POINT('Ctrl Pts',(17.5884257348914,-16.662620257991,1.90763710022151));
#144525=CARTESIAN_POINT('Ctrl Pts',(17.6632002791341,-16.6252041002441,
1.91182173531041));
#144526=CARTESIAN_POINT('Ctrl Pts',(17.7399490034736,-16.5913855369184,
1.91600637039932));
#144527=CARTESIAN_POINT('Ctrl Pts',(17.8182913485561,-16.5613771385535,
1.92019100548822));
#144528=CARTESIAN_POINT('Ctrl Pts',(17.8965221835584,-16.5314114532182,
1.92436968429646));
#144529=CARTESIAN_POINT('Ctrl Pts',(17.9763417078038,-16.5052453236658,
1.92854836310471));
#144530=CARTESIAN_POINT('Ctrl Pts',(18.0573458795832,-16.4830449171111,
1.93272704191295));
#144531=CARTESIAN_POINT('Ctrl Pts',(18.1398019751916,-16.4604465890842,
1.93698061962087));
#144532=CARTESIAN_POINT('Ctrl Pts',(18.2234851739771,-16.4419577675956,
1.94123419732878));
#144533=CARTESIAN_POINT('Ctrl Pts',(18.3079491747708,-16.427701940277,1.9454877750367));
#144534=CARTESIAN_POINT('Ctrl Pts',(18.3907756952209,-16.4137224867601,
1.94965888980394));
#144535=CARTESIAN_POINT('Ctrl Pts',(18.4743525389444,-16.403813444343,1.95383000457117));
#144536=CARTESIAN_POINT('Ctrl Pts',(18.5582464958779,-16.3980401910389,
1.95800111933841));
#144537=CARTESIAN_POINT('Ctrl Pts',(18.6421123018441,-16.392268874974,1.96217083447069));
#144538=CARTESIAN_POINT('Ctrl Pts',(18.7262945511255,-16.390630623423,1.96634054960296));
#144539=CARTESIAN_POINT('Ctrl Pts',(18.8103550385198,-16.3931389431834,
1.97051026473523));
#144540=CARTESIAN_POINT('Ctrl Pts',(18.8944125351178,-16.3956471737001,
1.9746798315128));
#144541=CARTESIAN_POINT('Ctrl Pts',(18.9783478186396,-16.4023016676252,
1.97884939829037));
#144542=CARTESIAN_POINT('Ctrl Pts',(19.0617241844762,-16.4130638332346,
1.98301896506794));
#144543=CARTESIAN_POINT('Ctrl Pts',(19.1480319248428,-16.4242043787102,
1.98733512688752));
#144544=CARTESIAN_POINT('Ctrl Pts',(19.2337401905731,-16.4397467505396,
1.99165128870711));
#144545=CARTESIAN_POINT('Ctrl Pts',(19.3183740371495,-16.4595901250586,
1.99596745052669));
#144546=CARTESIAN_POINT('Ctrl Pts',(19.400250979758,-16.4787871118715,2.00014301559772));
#144547=CARTESIAN_POINT('Ctrl Pts',(19.4811219861016,-16.5020090222104,
2.00431858066876));
#144548=CARTESIAN_POINT('Ctrl Pts',(19.5605725242511,-16.529113733137,2.00849414573979));
#144549=CARTESIAN_POINT('Ctrl Pts',(19.644035868025,-16.5575874207753,2.01288060593365));
#144550=CARTESIAN_POINT('Ctrl Pts',(19.7259309366168,-16.590346235569,2.01726706612751));
#144551=CARTESIAN_POINT('Ctrl Pts',(19.8058030522791,-16.6271692067754,
2.02165352632137));
#144552=CARTESIAN_POINT('Ctrl Pts',(19.8856751679415,-16.6639921779819,
2.02603998651523));
#144553=CARTESIAN_POINT('Ctrl Pts',(19.9635238523658,-16.7048789684718,
2.03042644670909));
#144554=CARTESIAN_POINT('Ctrl Pts',(20.0389283878907,-16.7495554711919,
2.03481290690295));
#144555=CARTESIAN_POINT('Ctrl Pts',(20.1108634458004,-16.7921763399234,
2.03899753937721));
#144556=CARTESIAN_POINT('Ctrl Pts',(20.1808420875151,-16.8384044873328,
2.04318217185146));
#144557=CARTESIAN_POINT('Ctrl Pts',(20.2484795854365,-16.8880349844786,
2.04736680432571));
#144558=CARTESIAN_POINT('Ctrl Pts',(20.3160208091885,-16.9375948383417,
2.05154548045877));
#144559=CARTESIAN_POINT('Ctrl Pts',(20.3812271405152,-16.9905471526885,
2.05572415659182));
#144560=CARTESIAN_POINT('Ctrl Pts',(20.4437401590352,-17.0466421363476,
2.05990283272488));
#144561=CARTESIAN_POINT('Ctrl Pts',(20.5073737154297,-17.1037426154257,
2.06415641109403));
#144562=CARTESIAN_POINT('Ctrl Pts',(20.568216035996,-17.1640992946966,2.06840998946317));
#144563=CARTESIAN_POINT('Ctrl Pts',(20.625921711991,-17.2274037470478,2.07266356783232));
#144564=CARTESIAN_POINT('Ctrl Pts',(20.6825086170737,-17.2894808820044,
2.07683467979464));
#144565=CARTESIAN_POINT('Ctrl Pts',(20.7360790916418,-17.3543921543138,
2.08100579175696));
#144566=CARTESIAN_POINT('Ctrl Pts',(20.7863436747178,-17.4218086914226,
2.08517690371928));
#144567=CARTESIAN_POINT('Ctrl Pts',(20.8365913907808,-17.4892026059304,
2.08934661600422));
#144568=CARTESIAN_POINT('Ctrl Pts',(20.8835351437711,-17.5590997471374,
2.09351632828917));
#144569=CARTESIAN_POINT('Ctrl Pts',(20.9269263843814,-17.6311389654154,
2.09768604057411));
#144570=CARTESIAN_POINT('Ctrl Pts',(20.970316080766,-17.7031756199314,2.10185560446557));
#144571=CARTESIAN_POINT('Ctrl Pts',(21.010153279513,-17.7773538054376,2.10602516835703));
#144572=CARTESIAN_POINT('Ctrl Pts',(21.0462340501421,-17.8532854340807,
2.1101947322485));
#144573=CARTESIAN_POINT('Ctrl Pts',(21.0835834150717,-17.9318868070124,
2.11451089735982));
#144574=CARTESIAN_POINT('Ctrl Pts',(21.1169070502971,-18.0123667468948,
2.11882706247114));
#144575=CARTESIAN_POINT('Ctrl Pts',(21.1460326532687,-18.094271325205,2.12314322758247));
#144576=CARTESIAN_POINT('Ctrl Pts',(21.1742094633,-18.1735077875708,2.12731878969955));
#144577=CARTESIAN_POINT('Ctrl Pts',(21.1984574604608,-18.2540770310568,
2.13149435181663));
#144578=CARTESIAN_POINT('Ctrl Pts',(21.2186717693381,-18.3355535719509,
2.13566991393371));
#144579=CARTESIAN_POINT('Ctrl Pts',(21.2399070877016,-18.4211454314377,
2.14005638054216));
#144580=CARTESIAN_POINT('Ctrl Pts',(21.2566904008667,-18.507738082136,2.1444428471506));
#144581=CARTESIAN_POINT('Ctrl Pts',(21.268961401442,-18.5948296020113,2.14882931375904));
#144582=CARTESIAN_POINT('Ctrl Pts',(21.2812324020172,-18.6819211218865,
2.15321578036749));
#144583=CARTESIAN_POINT('Ctrl Pts',(21.2889911145759,-18.769510926268,2.15760224697593));
#144584=CARTESIAN_POINT('Ctrl Pts',(21.2922402934534,-18.8570968865022,
2.16198871358438));
#144585=CARTESIAN_POINT('Ctrl Pts',(21.295340067666,-18.9406554442682,2.16617348044096));
#144586=CARTESIAN_POINT('Ctrl Pts',(21.2943474565442,-19.0245215346741,
2.17035824729755));
#144587=CARTESIAN_POINT('Ctrl Pts',(21.2892265251078,-19.1082606968682,
2.17454301415413));
#144588=CARTESIAN_POINT('Ctrl Pts',(21.2841129263152,-19.1918799532477,
2.17872178885763));
#144589=CARTESIAN_POINT('Ctrl Pts',(21.2748827772586,-19.2753721871246,
2.18290056356113));
#144590=CARTESIAN_POINT('Ctrl Pts',(21.2615521105126,-19.3583007859252,
2.18707933826462));
#144591=CARTESIAN_POINT('Ctrl Pts',(21.2482373459004,-19.4411304593154,
2.19125312811358));
#144592=CARTESIAN_POINT('Ctrl Pts',(21.2308318605286,-19.5233973824746,
2.19542691796253));
#144593=CARTESIAN_POINT('Ctrl Pts',(21.2094035420871,-19.6046693679211,
2.19960070781149));
#144594=CARTESIAN_POINT('Ctrl Pts',(21.1879892258981,-19.6858882465004,
2.20377177031347));
#144595=CARTESIAN_POINT('Ctrl Pts',(21.1625574130303,-19.766113034728,2.20794283281545));
#144596=CARTESIAN_POINT('Ctrl Pts',(21.1332269868316,-19.8449220938352,
2.21211389531743));
#144597=CARTESIAN_POINT('Ctrl Pts',(21.1039069279009,-19.9237032967282,
2.21628348349639));
#144598=CARTESIAN_POINT('Ctrl Pts',(21.0706911534139,-20.0010693338703,
2.22045307167534));
#144599=CARTESIAN_POINT('Ctrl Pts',(21.0337478603941,-20.0766153914174,
2.2246226598543));
#144600=CARTESIAN_POINT('Ctrl Pts',(20.9968065435593,-20.1521574078251,
2.22879202499201));
#144601=CARTESIAN_POINT('Ctrl Pts',(20.9561383080146,-20.2258792256777,
2.23296139012972));
#144602=CARTESIAN_POINT('Ctrl Pts',(20.9119581930118,-20.297398866319,2.23713075526742));
#144603=CARTESIAN_POINT('Ctrl Pts',(20.8677415456929,-20.3689776461936,
2.24130356803231));
#144604=CARTESIAN_POINT('Ctrl Pts',(20.8200074609641,-20.4383502197373,
2.2454763807972));
#144605=CARTESIAN_POINT('Ctrl Pts',(20.7690150631306,-20.5051624811435,
2.24964919356209));
#144606=CARTESIAN_POINT('Ctrl Pts',(20.7180006959783,-20.5720035276221,
2.2538238041215));
#144607=CARTESIAN_POINT('Ctrl Pts',(20.6637255152003,-20.636281711919,2.25799841468091));
#144608=CARTESIAN_POINT('Ctrl Pts',(20.606488337404,-20.6976767817342,2.26217302524032));
#144609=CARTESIAN_POINT('Ctrl Pts',(20.5491647021454,-20.7591645895589,
2.26635394160043));
#144610=CARTESIAN_POINT('Ctrl Pts',(20.4888704630452,-20.8177602628929,
2.27053485796053));
#144611=CARTESIAN_POINT('Ctrl Pts',(20.425940338613,-20.8731813788849,2.27471577432064));
#144612=CARTESIAN_POINT('Ctrl Pts',(20.3829942629984,-20.911003001828,2.2775690016384));
#144613=CARTESIAN_POINT('Ctrl Pts',(20.3388213089917,-20.9473469766555,
2.28042222895615));
#144614=CARTESIAN_POINT('Ctrl Pts',(20.2935357468249,-20.9821350335323,
2.28327545627391));
#144615=CARTESIAN_POINT('Origin',(18.734,-18.952,-1.76670989022851));
#144616=CARTESIAN_POINT('',(20.2935357468249,-20.9821350335323,3.1498113676566));
#144617=CARTESIAN_POINT('',(20.2933493665352,-20.9818838108336,3.08342410800429));
#144618=CARTESIAN_POINT('',(20.2935357468249,-20.9821350335323,-1.76670989022851));
#144619=CARTESIAN_POINT('',(16.1740010149448,-18.9497204131756,2.63329010980609));
#144620=CARTESIAN_POINT('Ctrl Pts',(16.1740010149447,-18.9497204131756,
2.63329010980609));
#144621=CARTESIAN_POINT('Ctrl Pts',(16.1740928743929,-18.8465613267996,
2.63841342883191));
#144622=CARTESIAN_POINT('Ctrl Pts',(16.1804238944876,-18.7436786900648,
2.64353674785773));
#144623=CARTESIAN_POINT('Ctrl Pts',(16.1928719236877,-18.6417289897893,
2.64866006688355));
#144624=CARTESIAN_POINT('Ctrl Pts',(16.2055250386107,-18.5380996318225,
2.6538677944185));
#144625=CARTESIAN_POINT('Ctrl Pts',(16.2244983314994,-18.4354341185118,
2.65907552195346));
#144626=CARTESIAN_POINT('Ctrl Pts',(16.249614957165,-18.3343990293583,2.66428324948841));
#144627=CARTESIAN_POINT('Ctrl Pts',(16.2576437833537,-18.3021019692125,
2.66594796113293));
#144628=CARTESIAN_POINT('Ctrl Pts',(16.2662999939976,-18.2699713447297,
2.66761267277746));
#144629=CARTESIAN_POINT('Ctrl Pts',(16.2755767948953,-18.2380284707337,
2.66927738442199));
#144630=CARTESIAN_POINT('Ctrl Pts',(16.2988961609904,-18.1577327328976,
2.67346201883521));
#144631=CARTESIAN_POINT('Ctrl Pts',(16.3261969265522,-18.0784312369419,
2.67764665324844));
#144632=CARTESIAN_POINT('Ctrl Pts',(16.3573766633345,-18.0005476808496,
2.68183128766167));
#144633=CARTESIAN_POINT('Ctrl Pts',(16.3885120196228,-17.9227749823538,
2.68600996576607));
#144634=CARTESIAN_POINT('Ctrl Pts',(16.4235152107072,-17.8464166382457,
2.69018864387046));
#144635=CARTESIAN_POINT('Ctrl Pts',(16.4622338002163,-17.7718820679608,
2.69436732197485));
#144636=CARTESIAN_POINT('Ctrl Pts',(16.5016463923759,-17.6960115195325,
2.6986208998552));
#144637=CARTESIAN_POINT('Ctrl Pts',(16.5449087556002,-17.6220312333017,
2.70287447773556));
#144638=CARTESIAN_POINT('Ctrl Pts',(16.5918084260802,-17.55035266182,2.70712805561592));
#144639=CARTESIAN_POINT('Ctrl Pts',(16.6377988552168,-17.4800637188786,
2.71129916961483));
#144640=CARTESIAN_POINT('Ctrl Pts',(16.6872865541291,-17.4119884433509,
2.71547028361374));
#144641=CARTESIAN_POINT('Ctrl Pts',(16.7400252973106,-17.346489213666,2.71964139761265));
#144642=CARTESIAN_POINT('Ctrl Pts',(16.7927463434996,-17.2810119628777,
2.72381111195413));
#144643=CARTESIAN_POINT('Ctrl Pts',(16.8487159791043,-17.2181093992062,
2.72798082629561));
#144644=CARTESIAN_POINT('Ctrl Pts',(16.9076465125813,-17.1581123393608,
2.73215054063709));
#144645=CARTESIAN_POINT('Ctrl Pts',(16.9665749490587,-17.0981174144666,
2.73632010660236));
#144646=CARTESIAN_POINT('Ctrl Pts',(17.0284637509528,-17.0410281154315,
2.74048967256763));
#144647=CARTESIAN_POINT('Ctrl Pts',(17.0929880053965,-16.987138774985,2.74465923853289));
#144648=CARTESIAN_POINT('Ctrl Pts',(17.1597808523047,-16.9313547524115,
2.7489754012471));
#144649=CARTESIAN_POINT('Ctrl Pts',(17.2293975200618,-16.8790002342604,
2.75329156396131));
#144650=CARTESIAN_POINT('Ctrl Pts',(17.3014414464082,-16.8303553571508,
2.75760772667552));
#144651=CARTESIAN_POINT('Ctrl Pts',(17.3711385501861,-16.7832950812869,
2.76178329088851));
#144652=CARTESIAN_POINT('Ctrl Pts',(17.4431067778018,-16.7397066785438,
2.76595885510149));
#144653=CARTESIAN_POINT('Ctrl Pts',(17.5169602827153,-16.6997978939377,
2.77013441931447));
#144654=CARTESIAN_POINT('Ctrl Pts',(17.5945439513522,-16.6578734121651,
2.77452088127929));
#144655=CARTESIAN_POINT('Ctrl Pts',(17.6742078257199,-16.6200102829155,
2.77890734324412));
#144656=CARTESIAN_POINT('Ctrl Pts',(17.7554809190364,-16.5863921694013,
2.78329380520894));
#144657=CARTESIAN_POINT('Ctrl Pts',(17.8367540123529,-16.5527740558871,
2.78768026717377));
#144658=CARTESIAN_POINT('Ctrl Pts',(17.9196357523207,-16.523401080228,2.79206672913859));
#144659=CARTESIAN_POINT('Ctrl Pts',(18.0036392138267,-16.4983958913426,
2.79645319110342));
#144660=CARTESIAN_POINT('Ctrl Pts',(18.0837775523632,-16.4745412280212,
2.80063782549362));
#144661=CARTESIAN_POINT('Ctrl Pts',(18.1652349468392,-16.4545724558021,
2.80482245988383));
#144662=CARTESIAN_POINT('Ctrl Pts',(18.247599691841,-16.4386327884245,2.80900709427403));
#144663=CARTESIAN_POINT('Ctrl Pts',(18.3298472008232,-16.4227158091904,
2.81318577235514));
#144664=CARTESIAN_POINT('Ctrl Pts',(18.4129990472135,-16.4108166300769,
2.81736445043625));
#144665=CARTESIAN_POINT('Ctrl Pts',(18.4966284631471,-16.4030286871971,
2.82154312851736));
#144666=CARTESIAN_POINT('Ctrl Pts',(18.5817568763298,-16.3951011510316,
2.82579670640351));
#144667=CARTESIAN_POINT('Ctrl Pts',(18.6673796862237,-16.3914338261788,
2.83005028428965));
#144668=CARTESIAN_POINT('Ctrl Pts',(18.7530359237116,-16.3920707756642,
2.8343038621758));
#144669=CARTESIAN_POINT('Ctrl Pts',(18.8370315478211,-16.3926953766405,
2.83847497615095));
#144670=CARTESIAN_POINT('Ctrl Pts',(18.921058833767,-16.3974588441841,2.84264609012611));
#144671=CARTESIAN_POINT('Ctrl Pts',(19.0046798014456,-16.4063502901834,
2.84681720410127));
#144672=CARTESIAN_POINT('Ctrl Pts',(19.0882727093013,-16.4152387525721,
2.85098691841886));
#144673=CARTESIAN_POINT('Ctrl Pts',(19.1714591125976,-16.4282523938203,
2.85515663273646));
#144674=CARTESIAN_POINT('Ctrl Pts',(19.2538051248627,-16.4453283756809,
2.85932634705406));
#144675=CARTESIAN_POINT('Ctrl Pts',(19.3361482069038,-16.4624037499049,
2.86349591299535));
#144676=CARTESIAN_POINT('Ctrl Pts',(19.4176505070951,-16.4835410830843,
2.86766547893664));
#144677=CARTESIAN_POINT('Ctrl Pts',(19.4978886690212,-16.508626491643,2.87183504487793));
#144678=CARTESIAN_POINT('Ctrl Pts',(19.580947905855,-16.5345938722575,2.87615120762017));
#144679=CARTESIAN_POINT('Ctrl Pts',(19.66265195286,-16.5647919650882,2.88046737036242));
#144680=CARTESIAN_POINT('Ctrl Pts',(19.7425506078301,-16.5990389566664,
2.88478353310466));
#144681=CARTESIAN_POINT('Ctrl Pts',(19.8198465724095,-16.6321703560494,
2.88895909729368));
#144682=CARTESIAN_POINT('Ctrl Pts',(19.8954525574107,-16.6690906702005,
2.89313466148269));
#144683=CARTESIAN_POINT('Ctrl Pts',(19.9689850307411,-16.7095879116796,
2.89731022567171));
#144684=CARTESIAN_POINT('Ctrl Pts',(20.046231454653,-16.7521305726411,2.90169668769057));
#144685=CARTESIAN_POINT('Ctrl Pts',(20.1211888996699,-16.7986206906169,
2.90608314970943));
#144686=CARTESIAN_POINT('Ctrl Pts',(20.1934479978659,-16.8487616536576,
2.91046961172828));
#144687=CARTESIAN_POINT('Ctrl Pts',(20.2657070960619,-16.8989026166982,
2.91485607374714));
#144688=CARTESIAN_POINT('Ctrl Pts',(20.3352674349797,-16.9526940096932,
2.919242535766));
#144689=CARTESIAN_POINT('Ctrl Pts',(20.401762322946,-17.0097927931959,2.92362899778485));
#144690=CARTESIAN_POINT('Ctrl Pts',(20.4651976823984,-17.0642643769006,
2.92781363217406));
#144691=CARTESIAN_POINT('Ctrl Pts',(20.5260796023552,-17.1219484370562,
2.93199826656327));
#144692=CARTESIAN_POINT('Ctrl Pts',(20.5840648143939,-17.1825763134451,
2.93618290095248));
#144693=CARTESIAN_POINT('Ctrl Pts',(20.6419674916593,-17.243117893555,2.94036157903251));
#144694=CARTESIAN_POINT('Ctrl Pts',(20.6969813355446,-17.3065946373119,
2.94454025711253));
#144695=CARTESIAN_POINT('Ctrl Pts',(20.7487967797138,-17.3726982756753,
2.94871893519256));
#144696=CARTESIAN_POINT('Ctrl Pts',(20.8015409785421,-17.439986774327,2.95297251307897));
#144697=CARTESIAN_POINT('Ctrl Pts',(20.8509706214137,-17.5099969539569,
2.95722609096537));
#144698=CARTESIAN_POINT('Ctrl Pts',(20.8967991444563,-17.5823650629678,
2.96147966885178));
#144699=CARTESIAN_POINT('Ctrl Pts',(20.9417391920986,-17.6533301748853,
2.96565078282566));
#144700=CARTESIAN_POINT('Ctrl Pts',(20.9832162459024,-17.7265621993701,
2.96982189679953));
#144701=CARTESIAN_POINT('Ctrl Pts',(21.0210023907229,-17.801686970939,2.97399301077341));
#144702=CARTESIAN_POINT('Ctrl Pts',(21.0587758560372,-17.8767865336643,
2.97816272508966));
#144703=CARTESIAN_POINT('Ctrl Pts',(21.0928606655495,-17.953777171463,2.9823324394059));
#144704=CARTESIAN_POINT('Ctrl Pts',(21.1230748017627,-18.0322600413256,
2.98650215372215));
#144705=CARTESIAN_POINT('Ctrl Pts',(21.153287862827,-18.11074011843,2.99067171966202));
#144706=CARTESIAN_POINT('Ctrl Pts',(21.1796303599629,-18.190711892398,2.99484128560189));
#144707=CARTESIAN_POINT('Ctrl Pts',(21.2019688964371,-18.2717577444622,
2.99901085154177));
#144708=CARTESIAN_POINT('Ctrl Pts',(21.2250928283449,-18.3556530688812,
3.00332701428548));
#144709=CARTESIAN_POINT('Ctrl Pts',(21.2439258622492,-18.4406988974017,
3.00764317702919));
#144710=CARTESIAN_POINT('Ctrl Pts',(21.2583771885884,-18.5264182690313,
3.0119593397729));
#144711=CARTESIAN_POINT('Ctrl Pts',(21.2723577644625,-18.6093453409698,
3.01613490396033));
#144712=CARTESIAN_POINT('Ctrl Pts',(21.2822377087348,-18.6929022752308,
3.02031046814777));
#144713=CARTESIAN_POINT('Ctrl Pts',(21.2879876706469,-18.7766518372396,
3.02448603233521));
#144714=CARTESIAN_POINT('Ctrl Pts',(21.2940280494849,-18.8646313908058,
3.02887249435706));
#144715=CARTESIAN_POINT('Ctrl Pts',(21.295510260803,-18.9528229589747,3.0332589563789));
#144716=CARTESIAN_POINT('Ctrl Pts',(21.2924621252161,-19.0407217776804,
3.03764541840075));
#144717=CARTESIAN_POINT('Ctrl Pts',(21.2894139896292,-19.128620596386,3.0420318804226));
#144718=CARTESIAN_POINT('Ctrl Pts',(21.2818356329245,-19.2162260941259,
3.04641834244445));
#144719=CARTESIAN_POINT('Ctrl Pts',(21.2698170137414,-19.303044260485,3.05080480446629));
#144720=CARTESIAN_POINT('Ctrl Pts',(21.2583547009867,-19.3858438700274,
3.05498823010072));
#144721=CARTESIAN_POINT('Ctrl Pts',(21.2428114366919,-19.4682355295024,
3.05917165573515));
#144722=CARTESIAN_POINT('Ctrl Pts',(21.2232272746467,-19.549785559507,3.06335508136958));
#144723=CARTESIAN_POINT('Ctrl Pts',(21.2036685685069,-19.6312295890686,
3.06753306929945));
#144724=CARTESIAN_POINT('Ctrl Pts',(21.1800794975091,-19.711833717846,3.07171105722931));
#144725=CARTESIAN_POINT('Ctrl Pts',(21.1525516402421,-19.7911709977603,
3.07588904515917));
#144726=CARTESIAN_POINT('Ctrl Pts',(21.1250513038486,-19.8704289605227,
3.08006285616107));
#144727=CARTESIAN_POINT('Ctrl Pts',(21.0936201503625,-19.9484221572867,
3.08423666716296));
#144728=CARTESIAN_POINT('Ctrl Pts',(21.0584001058537,-20.024736756109,3.08841047816485));
#144729=CARTESIAN_POINT('Ctrl Pts',(21.0232047055544,-20.1009979559936,
3.09258136866297));
#144730=CARTESIAN_POINT('Ctrl Pts',(20.9842258731267,-20.175582474819,3.09675225916109));
#144731=CARTESIAN_POINT('Ctrl Pts',(20.941653896439,-20.2480957810045,3.10092314965921));
#144732=CARTESIAN_POINT('Ctrl Pts',(20.8990871157836,-20.3206002367323,
3.10509353108814));
#144733=CARTESIAN_POINT('Ctrl Pts',(20.8529282822877,-20.3910335782582,
3.10926391251707));
#144734=CARTESIAN_POINT('Ctrl Pts',(20.8034134872385,-20.4590261506807,
3.11343429394599));
#144735=CARTESIAN_POINT('Ctrl Pts',(20.7539049126767,-20.5270101812736,
3.11760415145464));
#144736=CARTESIAN_POINT('Ctrl Pts',(20.7010414902595,-20.5925536836385,
3.12177400896329));
#144737=CARTESIAN_POINT('Ctrl Pts',(20.6451014452025,-20.6553177231934,
3.12594386647194));
#144738=CARTESIAN_POINT('Ctrl Pts',(20.5891189590868,-20.718129381092,3.13011688760277));
#144739=CARTESIAN_POINT('Ctrl Pts',(20.5300554962292,-20.7781570214064,
3.13428990873359));
#144740=CARTESIAN_POINT('Ctrl Pts',(20.4682278066355,-20.8350968946638,
3.13846292986442));
#144741=CARTESIAN_POINT('Ctrl Pts',(20.4121814661711,-20.8867124659967,
3.14224574246181));
#144742=CARTESIAN_POINT('Ctrl Pts',(20.3538643415153,-20.9357910227048,
3.14602855505921));
#144743=CARTESIAN_POINT('Ctrl Pts',(20.2935357468249,-20.9821350335323,
3.1498113676566));
#144744=CARTESIAN_POINT('Ctrl Pts',(20.2935357468249,-20.9821350335323,
2.34989189284213));
#144745=CARTESIAN_POINT('Ctrl Pts',(20.2268473385658,-21.0333646093295,
2.354061433181));
#144746=CARTESIAN_POINT('Ctrl Pts',(20.1576293985627,-21.0813067494096,
2.35823097351988));
#144747=CARTESIAN_POINT('Ctrl Pts',(20.086244279078,-21.1257146569181,2.36240051385875));
#144748=CARTESIAN_POINT('Ctrl Pts',(20.0113055277115,-21.172333240224,2.36677761862545));
#144749=CARTESIAN_POINT('Ctrl Pts',(19.9339786873142,-21.2150562657093,
2.37115472339215));
#144750=CARTESIAN_POINT('Ctrl Pts',(19.8547138950657,-21.2536516603097,
2.37553182815884));
#144751=CARTESIAN_POINT('Ctrl Pts',(19.7791007054641,-21.2904690265942,
2.37970728668516));
#144752=CARTESIAN_POINT('Ctrl Pts',(19.7017246343737,-21.3235305286003,
2.38388274521148));
#144753=CARTESIAN_POINT('Ctrl Pts',(19.6229967617461,-21.3526842269663,
2.38805820373779));
#144754=CARTESIAN_POINT('Ctrl Pts',(19.5442131942302,-21.3818585496922,
2.39223661613151));
#144755=CARTESIAN_POINT('Ctrl Pts',(19.4640763602644,-21.4071194301684,
2.39641502852523));
#144756=CARTESIAN_POINT('Ctrl Pts',(19.3830113934786,-21.4283651207233,
2.40059344091895));
#144757=CARTESIAN_POINT('Ctrl Pts',(19.3018201752775,-21.4496438995358,
2.40477836081522));
#144758=CARTESIAN_POINT('Ctrl Pts',(19.2196983897446,-21.4668949224409,
2.4089632807115));
#144759=CARTESIAN_POINT('Ctrl Pts',(19.1370795562275,-21.4800678138356,
2.41314820060778));
#144760=CARTESIAN_POINT('Ctrl Pts',(19.1253819370915,-21.4819329027009,
2.41374072409156));
#144761=CARTESIAN_POINT('Ctrl Pts',(19.1136743577112,-21.4837163248914,
2.41433324757534));
#144762=CARTESIAN_POINT('Ctrl Pts',(19.1019580505853,-21.4854180217661,
2.41492577105912));
#144763=CARTESIAN_POINT('Ctrl Pts',(19.0192128717128,-21.4974360758147,
2.41911040544304));
#144764=CARTESIAN_POINT('Ctrl Pts',(18.93572429724,-21.5054183621376,2.42329503982696));
#144765=CARTESIAN_POINT('Ctrl Pts',(18.8519204122536,-21.5092826938714,
2.42747967421088));
#144766=CARTESIAN_POINT('Ctrl Pts',(18.7682358117201,-21.5131415252074,
2.43165835228593));
#144767=CARTESIAN_POINT('Ctrl Pts',(18.6842372477561,-21.5128940235269,
2.43583703036098));
#144768=CARTESIAN_POINT('Ctrl Pts',(18.6003605130579,-21.5085094342736,
2.44001570843604));
#144769=CARTESIAN_POINT('Ctrl Pts',(18.5149803479444,-21.5040462543972,
2.44426928632372));
#144770=CARTESIAN_POINT('Ctrl Pts',(18.4297268997688,-21.4952961442208,
2.44852286421141));
#144771=CARTESIAN_POINT('Ctrl Pts',(18.3450626650517,-21.4822821481968,
2.4527764420991));
#144772=CARTESIAN_POINT('Ctrl Pts',(18.2620398119422,-21.4695204539125,
2.45694755606877));
#144773=CARTESIAN_POINT('Ctrl Pts',(18.1795840056904,-21.4526587990534,
2.46111867003844));
#144774=CARTESIAN_POINT('Ctrl Pts',(18.0981270507739,-21.4317712782518,
2.46528978400811));
#144775=CARTESIAN_POINT('Ctrl Pts',(18.0166974295207,-21.4108907664583,
2.46945949832045));
#144776=CARTESIAN_POINT('Ctrl Pts',(17.9362664391865,-21.3859871858384,
2.47362921263278));
#144777=CARTESIAN_POINT('Ctrl Pts',(17.8572543229418,-21.3571854435281,
2.47779892694512));
#144778=CARTESIAN_POINT('Ctrl Pts',(17.7782450182821,-21.3283847261057,
2.48196849288139));
#144779=CARTESIAN_POINT('Ctrl Pts',(17.7006549192466,-21.2956862811423,
2.48613805881767));
#144780=CARTESIAN_POINT('Ctrl Pts',(17.6248864697077,-21.2592640024329,
2.49030762475394));
#144781=CARTESIAN_POINT('Ctrl Pts',(17.5464540946263,-21.2215611611785,
2.49462378750282));
#144782=CARTESIAN_POINT('Ctrl Pts',(17.4699743261966,-21.1798679825075,
2.49893995025171));
#144783=CARTESIAN_POINT('Ctrl Pts',(17.3958663510849,-21.1344294576552,
2.5032561130006));
#144784=CARTESIAN_POINT('Ctrl Pts',(17.3241724357537,-21.0904710881461,
2.50743167718525));
#144785=CARTESIAN_POINT('Ctrl Pts',(17.2546985266634,-21.0430079392875,
2.5116072413699));
#144786=CARTESIAN_POINT('Ctrl Pts',(17.1877934784105,-20.9923052204496,
2.51578280555455));
#144787=CARTESIAN_POINT('Ctrl Pts',(17.1175092148079,-20.9390416275037,
2.52016926758555));
#144788=CARTESIAN_POINT('Ctrl Pts',(17.0500605848376,-20.8822029788446,
2.52455572961655));
#144789=CARTESIAN_POINT('Ctrl Pts',(16.985809772922,-20.8221419544914,2.52894219164755));
#144790=CARTESIAN_POINT('Ctrl Pts',(16.9215589610063,-20.7620809301381,
2.53332865367855));
#144791=CARTESIAN_POINT('Ctrl Pts',(16.8605063152546,-20.6987980004711,
2.53771511570955));
#144792=CARTESIAN_POINT('Ctrl Pts',(16.802965079949,-20.6326856153201,2.54210157774055));
#144793=CARTESIAN_POINT('Ctrl Pts',(16.7485317522925,-20.5701440813406,
2.54625111891253));
#144794=CARTESIAN_POINT('Ctrl Pts',(16.6970294692199,-20.5048282635504,
2.5504006600845));
#144795=CARTESIAN_POINT('Ctrl Pts',(16.6487573722081,-20.4370465256145,
2.55455020125647));
#144796=CARTESIAN_POINT('Ctrl Pts',(16.6005493742832,-20.3693547930394,
2.55869423237572));
#144797=CARTESIAN_POINT('Ctrl Pts',(16.5555633203296,-20.2992040148308,
2.56283826349496));
#144798=CARTESIAN_POINT('Ctrl Pts',(16.514059720175,-20.2269373137572,2.5669822946142));
#144799=CARTESIAN_POINT('Ctrl Pts',(16.4725982721948,-20.154744008692,2.5711221169438));
#144800=CARTESIAN_POINT('Ctrl Pts',(16.4346124893252,-20.0804394498693,
2.57526193927339));
#144801=CARTESIAN_POINT('Ctrl Pts',(16.4003201033268,-20.0043963796323,
2.57940176160299));
#144802=CARTESIAN_POINT('Ctrl Pts',(16.3660518421397,-19.9284068059566,
2.58353867155335));
#144803=CARTESIAN_POINT('Ctrl Pts',(16.3354720095443,-19.8506815753093,
2.58767558150371));
#144804=CARTESIAN_POINT('Ctrl Pts',(16.3087521158423,-19.7716174109842,
2.59181249145407));
#144805=CARTESIAN_POINT('Ctrl Pts',(16.2820372325143,-19.6925680723558,
2.59594862567282));
#144806=CARTESIAN_POINT('Ctrl Pts',(16.2591810094483,-19.6121807387927,
2.60008475989157));
#144807=CARTESIAN_POINT('Ctrl Pts',(16.2403061251851,-19.5308703297896,
2.60422089411032));
#144808=CARTESIAN_POINT('Ctrl Pts',(16.2214331728165,-19.4495682431231,
2.60835660498473));
#144809=CARTESIAN_POINT('Ctrl Pts',(16.2065408484312,-19.3673437264668,
2.61249231585914));
#144810=CARTESIAN_POINT('Ctrl Pts',(16.1957010120584,-19.2846232821293,
2.61662802673355));
#144811=CARTESIAN_POINT('Ctrl Pts',(16.1848552750847,-19.2018578094073,
2.62076598885772));
#144812=CARTESIAN_POINT('Ctrl Pts',(16.1780664813587,-19.1185963356398,
2.62490395098188));
#144813=CARTESIAN_POINT('Ctrl Pts',(16.1753546619781,-19.0352708485527,
2.62904191310604));
#144814=CARTESIAN_POINT('Ctrl Pts',(16.1744266413966,-19.0067557610314,
2.63045797866119));
#144815=CARTESIAN_POINT('Ctrl Pts',(16.1739756253558,-18.9782331861948,
2.63187404421635));
#144816=CARTESIAN_POINT('Ctrl Pts',(16.1740010149441,-18.949720413872,2.6332901097715));
#144817=CARTESIAN_POINT('',(16.1740009418753,-18.9541959965583,2.56670989022851));
#144818=CARTESIAN_POINT('Ctrl Pts',(20.2935357468249,-20.9821350335323,
2.28327545627391));
#144819=CARTESIAN_POINT('Ctrl Pts',(20.262379265198,-21.006069228076,2.28523847760454));
#144820=CARTESIAN_POINT('Ctrl Pts',(20.2306962676017,-21.0292671335208,
2.28720149893518));
#144821=CARTESIAN_POINT('Ctrl Pts',(20.1985254700657,-21.0517059669222,
2.28916452026582));
#144822=CARTESIAN_POINT('Ctrl Pts',(20.1299459675163,-21.0995395349505,
2.29334915467529));
#144823=CARTESIAN_POINT('Ctrl Pts',(20.0588929044663,-21.1440987240594,
2.29753378908477));
#144824=CARTESIAN_POINT('Ctrl Pts',(19.9857121094434,-21.1851181775877,
2.30171842349424));
#144825=CARTESIAN_POINT('Ctrl Pts',(19.9126354781746,-21.226079245029,2.30589710159743));
#144826=CARTESIAN_POINT('Ctrl Pts',(19.8374375284691,-21.2635103616748,
2.31007577970061));
#144827=CARTESIAN_POINT('Ctrl Pts',(19.7604940332823,-21.2971886916911,
2.3142544578038));
#144828=CARTESIAN_POINT('Ctrl Pts',(19.6821713816853,-21.3314706813749,
2.31850803568478));
#144829=CARTESIAN_POINT('Ctrl Pts',(19.6020403867589,-21.3618637479467,
2.32276161356576));
#144830=CARTESIAN_POINT('Ctrl Pts',(19.5205248076212,-21.3881811769646,
2.32701519144673));
#144831=CARTESIAN_POINT('Ctrl Pts',(19.4405895664662,-21.413988391455,2.33118630545076));
#144832=CARTESIAN_POINT('Ctrl Pts',(19.3593234056757,-21.4358764386427,
2.33535741945479));
#144833=CARTESIAN_POINT('Ctrl Pts',(19.2771455317525,-21.4537179959654,
2.33952853345882));
#144834=CARTESIAN_POINT('Ctrl Pts',(19.194995233359,-21.4715535663921,2.34369824780777));
#144835=CARTESIAN_POINT('Ctrl Pts',(19.1119342786071,-21.485345246116,2.34786796215672));
#144836=CARTESIAN_POINT('Ctrl Pts',(19.0283943159569,-21.4950163166469,
2.35203767650567));
#144837=CARTESIAN_POINT('Ctrl Pts',(18.9448573259675,-21.5046870430453,
2.35620724248077));
#144838=CARTESIAN_POINT('Ctrl Pts',(18.8608418190481,-21.5102373997256,
2.36037680845588));
#144839=CARTESIAN_POINT('Ctrl Pts',(18.7767854909901,-21.5116424363103,
2.36454637443098));
#144840=CARTESIAN_POINT('Ctrl Pts',(18.6897738473697,-21.5130968722274,
2.36886253714067));
#144841=CARTESIAN_POINT('Ctrl Pts',(18.6027189860106,-21.5101090568378,
2.37317869985036));
#144842=CARTESIAN_POINT('Ctrl Pts',(18.5161054386262,-21.5027100893915,
2.37749486256005));
#144843=CARTESIAN_POINT('Ctrl Pts',(18.4323133171285,-21.4955521424197,
2.3816704267887));
#144844=CARTESIAN_POINT('Ctrl Pts',(18.3489346599974,-21.4842661264524,
2.38584599101735));
#144845=CARTESIAN_POINT('Ctrl Pts',(18.266400191337,-21.4689327402492,2.390021555246));
#144846=CARTESIAN_POINT('Ctrl Pts',(18.1796971048713,-21.452824901532,2.39440801719621));
#144847=CARTESIAN_POINT('Ctrl Pts',(18.0939262957253,-21.4322502184638,
2.39879447914641));
#144848=CARTESIAN_POINT('Ctrl Pts',(18.0095696123222,-21.4073616054278,
2.40318094109662));
#144849=CARTESIAN_POINT('Ctrl Pts',(17.9252129289191,-21.3824729923918,
2.40756740304683));
#144850=CARTESIAN_POINT('Ctrl Pts',(17.8422708932844,-21.3532707138249,
2.41195386499704));
#144851=CARTESIAN_POINT('Ctrl Pts',(17.7611994326681,-21.3199651720832,
2.41634032694725));
#144852=CARTESIAN_POINT('Ctrl Pts',(17.6838581936353,-21.288192069127,2.42052496109126));
#144853=CARTESIAN_POINT('Ctrl Pts',(17.6079312972239,-21.2525667345156,
2.42470959523527));
#144854=CARTESIAN_POINT('Ctrl Pts',(17.5338290567893,-21.2132363226944,
2.42889422937928));
#144855=CARTESIAN_POINT('Ctrl Pts',(17.4598322918057,-21.1739618928909,
2.4330729072098));
#144856=CARTESIAN_POINT('Ctrl Pts',(17.3876554268637,-21.1309930749775,
2.43725158504032));
#144857=CARTESIAN_POINT('Ctrl Pts',(17.3176892303927,-21.0845252176456,
2.44143026287085));
#144858=CARTESIAN_POINT('Ctrl Pts',(17.246468934763,-21.0372244537998,2.44568384081909));
#144859=CARTESIAN_POINT('Ctrl Pts',(17.1775397859107,-20.9862981588104,
2.44993741876734));
#144860=CARTESIAN_POINT('Ctrl Pts',(17.1112881539936,-20.9320015820273,
2.45419099671558));
#144861=CARTESIAN_POINT('Ctrl Pts',(17.046320944286,-20.8787576544711,2.4583621104312));
#144862=CARTESIAN_POINT('Ctrl Pts',(16.983928731977,-20.8222732634782,2.46253322414681));
#144863=CARTESIAN_POINT('Ctrl Pts',(16.9244454837175,-20.762831978015,2.46670433786243));
#144864=CARTESIAN_POINT('Ctrl Pts',(16.8649821956771,-20.7034106386898,
2.4708740519177));
#144865=CARTESIAN_POINT('Ctrl Pts',(16.8084262582069,-20.641034700359,2.47504376597298));
#144866=CARTESIAN_POINT('Ctrl Pts',(16.7550758225426,-20.5760255847352,
2.47921348002825));
#144867=CARTESIAN_POINT('Ctrl Pts',(16.7017272853469,-20.5110187824527,
2.48338304570478));
#144868=CARTESIAN_POINT('Ctrl Pts',(16.651584314341,-20.4433793453335,2.4875526113813));
#144869=CARTESIAN_POINT('Ctrl Pts',(16.6049048052798,-20.3734618010412,
2.49172217705783));
#144870=CARTESIAN_POINT('Ctrl Pts',(16.5565840957098,-20.3010860323251,
2.4960383401054));
#144871=CARTESIAN_POINT('Ctrl Pts',(16.5119752240842,-20.2262694173157,
2.50035450315297));
#144872=CARTESIAN_POINT('Ctrl Pts',(16.4713143087945,-20.1494362040685,
2.50467066620054));
#144873=CARTESIAN_POINT('Ctrl Pts',(16.4319779239082,-20.0751058347982,
2.50884623012138));
#144874=CARTESIAN_POINT('Ctrl Pts',(16.3963363916713,-19.9988886782757,
2.51302179404221));
#144875=CARTESIAN_POINT('Ctrl Pts',(16.3645549999889,-19.9211905859647,
2.51719735796305));
#144876=CARTESIAN_POINT('Ctrl Pts',(16.3311683990456,-19.8395681312915,
2.52158382057399));
#144877=CARTESIAN_POINT('Ctrl Pts',(16.3020423326888,-19.7563117555003,
2.52597028318493));
#144878=CARTESIAN_POINT('Ctrl Pts',(16.2773090396202,-19.6719093867897,
2.53035674579587));
#144879=CARTESIAN_POINT('Ctrl Pts',(16.2525757465516,-19.5875070180792,
2.53474320840681));
#144880=CARTESIAN_POINT('Ctrl Pts',(16.2322352869843,-19.5019592385255,
2.53912967101775));
#144881=CARTESIAN_POINT('Ctrl Pts',(16.2163575306375,-19.4157632978817,
2.54351613362869));
#144882=CARTESIAN_POINT('Ctrl Pts',(16.193544110504,-19.2919155599045,2.54981867488562));
#144883=CARTESIAN_POINT('Ctrl Pts',(16.1798641823048,-19.1663368454762,
2.55612121614255));
#144884=CARTESIAN_POINT('Ctrl Pts',(16.1755170133934,-19.040118143674,2.56242375739948));
#144885=CARTESIAN_POINT('Ctrl Pts',(16.1745315620426,-19.0115058691761,
2.56385246834249));
#144886=CARTESIAN_POINT('Ctrl Pts',(16.1740255308992,-18.9828608310217,
2.5652811792855));
#144887=CARTESIAN_POINT('Ctrl Pts',(16.1740009418753,-18.9541959965583,
2.56670989022851));
#144888=CARTESIAN_POINT('Ctrl Pts',(16.172685086933,-18.9541844540912,2.56671052146184));
#144889=CARTESIAN_POINT('Ctrl Pts',(16.1790130664392,-18.2584131946872,
2.60137099441126));
#144890=CARTESIAN_POINT('Ctrl Pts',(16.8320815170599,-16.7012241087188,
2.67842340292117));
#144891=CARTESIAN_POINT('Ctrl Pts',(19.4673983706617,-16.0150936874702,
2.79786774699155));
#144892=CARTESIAN_POINT('Ctrl Pts',(21.600448060805,-17.9789802882804,2.92504355367299));
#144893=CARTESIAN_POINT('Ctrl Pts',(21.2286613153073,-20.1169976411095,
3.0202290073439));
#144894=CARTESIAN_POINT('Ctrl Pts',(20.4604812917091,-20.8561430802638,
3.07302252545434));
#144895=CARTESIAN_POINT('Ctrl Pts',(20.293349366535,-20.9818838108338,3.08342410800431));
#144896=CARTESIAN_POINT('Origin',(18.734,-18.952,-1.76670989022851));
#144897=CARTESIAN_POINT('',(20.2935357468249,-20.9821350335323,3.94993168858525));
#144898=CARTESIAN_POINT('',(20.2935357468249,-20.9821350335323,3.88329345209041));
#144899=CARTESIAN_POINT('',(20.2935357468249,-20.9821350335323,-1.76670989022851));
#144900=CARTESIAN_POINT('',(16.1740000028035,-18.9521198080497,3.43329010980363));
#144901=CARTESIAN_POINT('Ctrl Pts',(16.1740000028035,-18.9521198080497,
3.43329010980363));
#144902=CARTESIAN_POINT('Ctrl Pts',(16.173996094898,-18.8686175883754,3.43746913841141));
#144903=CARTESIAN_POINT('Ctrl Pts',(16.1780820066338,-18.7849577973269,
3.4416481670192));
#144904=CARTESIAN_POINT('Ctrl Pts',(16.1862780259001,-18.7015748760835,
3.44582719562698));
#144905=CARTESIAN_POINT('Ctrl Pts',(16.1944623792895,-18.6183106386623,
3.45000027597724));
#144906=CARTESIAN_POINT('Ctrl Pts',(16.2067451760218,-18.5353229435673,
3.45417335632751));
#144907=CARTESIAN_POINT('Ctrl Pts',(16.2230946976723,-18.4530465324877,
3.45834643667777));
#144908=CARTESIAN_POINT('Ctrl Pts',(16.2396087147061,-18.369942324114,3.46256150311587));
#144909=CARTESIAN_POINT('Ctrl Pts',(16.2602717621694,-18.2875642714266,
3.46677656955396));
#144910=CARTESIAN_POINT('Ctrl Pts',(16.2849973159137,-18.2063554108437,
3.47099163599205));
#144911=CARTESIAN_POINT('Ctrl Pts',(16.3094325809408,-18.1260999774803,
3.47515721572334));
#144912=CARTESIAN_POINT('Ctrl Pts',(16.3378353258575,-18.0469868800097,
3.47932279545462));
#144913=CARTESIAN_POINT('Ctrl Pts',(16.3700710228284,-17.9694320426107,
3.4834883751859));
#144914=CARTESIAN_POINT('Ctrl Pts',(16.4022960455082,-17.8919028861488,
3.48765257555781));
#144915=CARTESIAN_POINT('Ctrl Pts',(16.4383513227395,-17.8159313907882,
3.49181677592972));
#144916=CARTESIAN_POINT('Ctrl Pts',(16.4780536821042,-17.7419147919373,
3.49598097630164));
#144917=CARTESIAN_POINT('Ctrl Pts',(16.5177548909312,-17.667900338019,3.50014505599887));
#144918=CARTESIAN_POINT('Ctrl Pts',(16.561102752779,-17.5958410741347,3.50430913569611));
#144919=CARTESIAN_POINT('Ctrl Pts',(16.6078681568274,-17.5261096166088,
3.50847321539335));
#144920=CARTESIAN_POINT('Ctrl Pts',(16.6556310871524,-17.4548907569615,
3.51272611670991));
#144921=CARTESIAN_POINT('Ctrl Pts',(16.7069587733462,-17.3861005826234,
3.51697901802647));
#144922=CARTESIAN_POINT('Ctrl Pts',(16.7615616490752,-17.320103265583,3.52123191934302));
#144923=CARTESIAN_POINT('Ctrl Pts',(16.815101261178,-17.255391092332,3.52540200532769));
#144924=CARTESIAN_POINT('Ctrl Pts',(16.8717892886061,-17.1933642853471,
3.52957209131236));
#144925=CARTESIAN_POINT('Ctrl Pts',(16.9313144499797,-17.134329840772,3.53374217729703));
#144926=CARTESIAN_POINT('Ctrl Pts',(16.9926128107595,-17.0735368147895,
3.53803648627953));
#144927=CARTESIAN_POINT('Ctrl Pts',(17.0569196193486,-17.0159176096088,
3.54233079526203));
#144928=CARTESIAN_POINT('Ctrl Pts',(17.1238587796064,-16.9617625140729,
3.54662510424453));
#144929=CARTESIAN_POINT('Ctrl Pts',(17.1907979398642,-16.9076074185369,
3.55091941322703));
#144930=CARTESIAN_POINT('Ctrl Pts',(17.2603689845986,-16.8569166856669,
3.55521372220953));
#144931=CARTESIAN_POINT('Ctrl Pts',(17.3321657913458,-16.809930708066,3.55950803119203));
#144932=CARTESIAN_POINT('Ctrl Pts',(17.4021289421208,-16.7641447297734,
3.56369266558497));
#144933=CARTESIAN_POINT('Ctrl Pts',(17.4744678068902,-16.7217048000894,
3.5678772999779));
#144934=CARTESIAN_POINT('Ctrl Pts',(17.5488288662328,-16.6828659396842,
3.57206193437084));
#144935=CARTESIAN_POINT('Ctrl Pts',(17.6230840818116,-16.6440823615896,
3.57624061245467));
#144936=CARTESIAN_POINT('Ctrl Pts',(17.6993553703909,-16.6088898827214,
3.5804192905385));
#144937=CARTESIAN_POINT('Ctrl Pts',(17.7772605377961,-16.5775001365631,
3.58459796862233));
#144938=CARTESIAN_POINT('Ctrl Pts',(17.8565620993404,-16.5455477517632,
3.58885154650779));
#144939=CARTESIAN_POINT('Ctrl Pts',(17.9375562869753,-16.5175360325719,
3.59310512439325));
#144940=CARTESIAN_POINT('Ctrl Pts',(18.0198140087904,-16.4936390887504,
3.59735870227872));
#144941=CARTESIAN_POINT('Ctrl Pts',(18.1004770041527,-16.4702054338167,
3.60152981625656));
#144942=CARTESIAN_POINT('Ctrl Pts',(18.1823545166279,-16.4507285663625,
3.60570093023439));
#144943=CARTESIAN_POINT('Ctrl Pts',(18.2650237601176,-16.4353233647475,
3.60987204421223));
#144944=CARTESIAN_POINT('Ctrl Pts',(18.3476652631442,-16.4199233324967,
3.61404175853249));
#144945=CARTESIAN_POINT('Ctrl Pts',(18.4310975176832,-16.408592336823,3.61821147285275));
#144946=CARTESIAN_POINT('Ctrl Pts',(18.5148867965883,-16.4013943064263,
3.622381187173));
#144947=CARTESIAN_POINT('Ctrl Pts',(18.5986730939112,-16.3941965321664,
3.62655075311693));
#144948=CARTESIAN_POINT('Ctrl Pts',(18.6828159319226,-16.3911314692988,
3.63072031906086));
#144949=CARTESIAN_POINT('Ctrl Pts',(18.766877068662,-16.3922111223079,3.63488988500479));
#144950=CARTESIAN_POINT('Ctrl Pts',(18.8538936912736,-16.3933287345849,
3.63920604774384));
#144951=CARTESIAN_POINT('Ctrl Pts',(18.9408222331035,-16.398887935209,3.6435222104829));
#144952=CARTESIAN_POINT('Ctrl Pts',(19.027179293109,-16.4088433193977,3.64783837322195));
#144953=CARTESIAN_POINT('Ctrl Pts',(19.110723280963,-16.418474407993,3.65201393741352));
#144954=CARTESIAN_POINT('Ctrl Pts',(19.1937319902678,-16.4322195436239,
3.65618950160508));
#144955=CARTESIAN_POINT('Ctrl Pts',(19.2757772698982,-16.4499853338116,
3.66036506579664));
#144956=CARTESIAN_POINT('Ctrl Pts',(19.3619664615662,-16.4686484318293,
3.66475152780944));
#144957=CARTESIAN_POINT('Ctrl Pts',(19.4470917766262,-16.4917488722623,
3.66913798982225));
#144958=CARTESIAN_POINT('Ctrl Pts',(19.5306760960807,-16.5191195676866,
3.67352445183505));
#144959=CARTESIAN_POINT('Ctrl Pts',(19.6142604155353,-16.5464902631109,
3.67791091384785));
#144960=CARTESIAN_POINT('Ctrl Pts',(19.6963032254015,-16.578130933778,3.68229737586066));
#144961=CARTESIAN_POINT('Ctrl Pts',(19.7763550154477,-16.6138177954293,
3.68668383787346));
#144962=CARTESIAN_POINT('Ctrl Pts',(19.8527235039631,-16.647862651673,3.69086847226646));
#144963=CARTESIAN_POINT('Ctrl Pts',(19.9275644240484,-16.6857162600702,
3.69505310665946));
#144964=CARTESIAN_POINT('Ctrl Pts',(20.0004719903204,-16.7272194045853,
3.69923774105246));
#144965=CARTESIAN_POINT('Ctrl Pts',(20.0732757816959,-16.7686634745112,
3.70341641913635));
#144966=CARTESIAN_POINT('Ctrl Pts',(20.1441512890029,-16.813746536681,3.70759509722024));
#144967=CARTESIAN_POINT('Ctrl Pts',(20.2127136875159,-16.8622617794678,
3.71177377530413));
#144968=CARTESIAN_POINT('Ctrl Pts',(20.2825050177484,-16.9116466231151,
3.71602735318958));
#144969=CARTESIAN_POINT('Ctrl Pts',(20.3498990582277,-16.964587704994,3.72028093107503));
#144970=CARTESIAN_POINT('Ctrl Pts',(20.4145171508852,-17.0208184690245,
3.72453450896048));
#144971=CARTESIAN_POINT('Ctrl Pts',(20.4778824957237,-17.0759590899682,
3.72870562293838));
#144972=CARTESIAN_POINT('Ctrl Pts',(20.5385782035453,-17.1342626616187,
3.73287673691628));
#144973=CARTESIAN_POINT('Ctrl Pts',(20.5962788337327,-17.1954358692518,
3.73704785089418));
#144974=CARTESIAN_POINT('Ctrl Pts',(20.6539601019164,-17.2565885496243,
3.7412175652145));
#144975=CARTESIAN_POINT('Ctrl Pts',(20.7086479730736,-17.3206086192034,
3.74538727953482));
#144976=CARTESIAN_POINT('Ctrl Pts',(20.7600539250065,-17.3871659854905,
3.74955699385514));
#144977=CARTESIAN_POINT('Ctrl Pts',(20.811458047695,-17.4537209833809,3.75372655979912));
#144978=CARTESIAN_POINT('Ctrl Pts',(20.8595802028305,-17.5228127338603,
3.75789612574311));
#144979=CARTESIAN_POINT('Ctrl Pts',(20.9041730844802,-17.5940792425927,
3.76206569168709));
#144980=CARTESIAN_POINT('Ctrl Pts',(20.9503337968388,-17.6678513938574,
3.76638185442608));
#144981=CARTESIAN_POINT('Ctrl Pts',(20.9927121598376,-17.7439536306547,
3.77069801716506));
#144982=CARTESIAN_POINT('Ctrl Pts',(21.0310846958974,-17.8219549124597,
3.77501417990405));
#144983=CARTESIAN_POINT('Ctrl Pts',(21.06820725063,-17.8974153107121,3.77918974409567));
#144984=CARTESIAN_POINT('Ctrl Pts',(21.1015808067413,-17.9746524800457,
3.78336530828729));
#144985=CARTESIAN_POINT('Ctrl Pts',(21.1310521424428,-18.0532558615431,
3.78754087247891));
#144986=CARTESIAN_POINT('Ctrl Pts',(21.1620120052503,-18.1358293129816,
3.79192733449158));
#144987=CARTESIAN_POINT('Ctrl Pts',(21.1886649090815,-18.2199100618434,
3.79631379650424));
#144988=CARTESIAN_POINT('Ctrl Pts',(21.2108930925539,-18.3050064853038,
3.80070025851691));
#144989=CARTESIAN_POINT('Ctrl Pts',(21.2331212760262,-18.3901029087642,
3.80508672052957));
#144990=CARTESIAN_POINT('Ctrl Pts',(21.2509246961549,-18.4762144232225,
3.80947318254223));
#144991=CARTESIAN_POINT('Ctrl Pts',(21.2642482087236,-18.5628419315355,
3.8138596445549));
#144992=CARTESIAN_POINT('Ctrl Pts',(21.2769586867287,-18.645483579777,3.818044278948));
#144993=CARTESIAN_POINT('Ctrl Pts',(21.285639763102,-18.7289023900137,3.82222891334111));
#144994=CARTESIAN_POINT('Ctrl Pts',(21.2902056694013,-18.8126709803349,
3.82641354773422));
#144995=CARTESIAN_POINT('Ctrl Pts',(21.2947650766981,-18.8963203364363,
3.83059222581822));
#144996=CARTESIAN_POINT('Ctrl Pts',(21.2952209238071,-18.9803180282762,
3.83477090390223));
#144997=CARTESIAN_POINT('Ctrl Pts',(21.2915388082527,-19.0642285359493,
3.83894958198623));
#144998=CARTESIAN_POINT('Ctrl Pts',(21.2877906934233,-19.1496430791655,
3.84320315987165));
#144999=CARTESIAN_POINT('Ctrl Pts',(21.2797547375529,-19.2349668053837,
3.84745673775707));
#145000=CARTESIAN_POINT('Ctrl Pts',(21.2674501116906,-19.319737041342,3.85171031564249));
#145001=CARTESIAN_POINT('Ctrl Pts',(21.2553840350109,-19.4028638408623,
3.85588142962051));
#145002=CARTESIAN_POINT('Ctrl Pts',(21.2392133934507,-19.4854579433579,
3.86005254359852));
#145003=CARTESIAN_POINT('Ctrl Pts',(21.2190086634415,-19.5670869390749,
3.86422365757654));
#145004=CARTESIAN_POINT('Ctrl Pts',(21.1988107133246,-19.648688543394,3.86839337189697));
#145005=CARTESIAN_POINT('Ctrl Pts',(21.1745814736228,-19.7293252379223,
3.87256308621741));
#145006=CARTESIAN_POINT('Ctrl Pts',(21.1464423282955,-19.8085757483422,
3.87673280053784));
#145007=CARTESIAN_POINT('Ctrl Pts',(21.1183041842799,-19.8878234386887,
3.88090236648194));
#145008=CARTESIAN_POINT('Ctrl Pts',(21.0862565659976,-19.9656846097689,
3.88507193242604));
#145009=CARTESIAN_POINT('Ctrl Pts',(21.0504699913875,-20.0417553757616,
3.88924149837014));
#145010=CARTESIAN_POINT('Ctrl Pts',(21.0134252049627,-20.1205006960409,
3.89355766110899));
#145011=CARTESIAN_POINT('Ctrl Pts',(20.9723738713789,-20.1973268901837,
3.89787382384784));
#145012=CARTESIAN_POINT('Ctrl Pts',(20.9275574633286,-20.2718127348512,
3.90218998658669));
#145013=CARTESIAN_POINT('Ctrl Pts',(20.8842009450553,-20.3438722109655,
3.90636555077843));
#145014=CARTESIAN_POINT('Ctrl Pts',(20.8373211816344,-20.413741105018,3.91054111497017));
#145015=CARTESIAN_POINT('Ctrl Pts',(20.7871804520949,-20.4810683539775,
3.91471667916191));
#145016=CARTESIAN_POINT('Ctrl Pts',(20.734507233507,-20.5517961422233,3.91910314117432));
#145017=CARTESIAN_POINT('Ctrl Pts',(20.6782353411158,-20.6197183310684,
3.92348960318672));
#145018=CARTESIAN_POINT('Ctrl Pts',(20.6187144099127,-20.6844697957158,
3.92787606519912));
#145019=CARTESIAN_POINT('Ctrl Pts',(20.5591934787095,-20.7492212603632,
3.93226252721153));
#145020=CARTESIAN_POINT('Ctrl Pts',(20.4964239761435,-20.8108016487773,
3.93664898922393));
#145021=CARTESIAN_POINT('Ctrl Pts',(20.4307957154099,-20.8688944415817,
3.94103545123633));
#145022=CARTESIAN_POINT('Ctrl Pts',(20.3864285555263,-20.9081673431888,
3.94400086368597));
#145023=CARTESIAN_POINT('Ctrl Pts',(20.3406387761084,-20.9459508109373,
3.94696627613561));
#145024=CARTESIAN_POINT('Ctrl Pts',(20.2935357468249,-20.9821350335323,
3.94993168858525));
#145025=CARTESIAN_POINT('Ctrl Pts',(20.2935357468249,-20.9821350335323,
3.1498113676566));
#145026=CARTESIAN_POINT('Ctrl Pts',(20.2269038271573,-21.0333212151827,
3.15398942064128));
#145027=CARTESIAN_POINT('Ctrl Pts',(20.1578180813607,-21.0811707044176,
3.15816747362595));
#145028=CARTESIAN_POINT('Ctrl Pts',(20.0866541319508,-21.1254596382994,
3.16234552661063));
#145029=CARTESIAN_POINT('Ctrl Pts',(20.0153772946765,-21.1698188280228,
3.16653020726961));
#145030=CARTESIAN_POINT('Ctrl Pts',(19.9420160778716,-21.2106059717294,
3.17071488792859));
#145031=CARTESIAN_POINT('Ctrl Pts',(19.8669695219043,-21.247643714176,3.17489956858757));
#145032=CARTESIAN_POINT('Ctrl Pts',(19.8485514193241,-21.2567336041907,
3.17592658277429));
#145033=CARTESIAN_POINT('Ctrl Pts',(19.8300318898626,-21.2655978908399,
3.176953596961));
#145034=CARTESIAN_POINT('Ctrl Pts',(19.8114169849418,-21.2742344068933,
3.17798061114772));
#145035=CARTESIAN_POINT('Ctrl Pts',(19.7355693750926,-21.3094244389056,
3.18216524554016));
#145036=CARTESIAN_POINT('Ctrl Pts',(19.6578547653244,-21.3409601078314,
3.1863498799326));
#145037=CARTESIAN_POINT('Ctrl Pts',(19.578659830513,-21.3686401823022,3.19053451432504));
#145038=CARTESIAN_POINT('Ctrl Pts',(19.4995776198891,-21.3962808576131,
3.19471319240837));
#145039=CARTESIAN_POINT('Ctrl Pts',(19.4190197000617,-21.4200766888,3.1988918704917));
#145040=CARTESIAN_POINT('Ctrl Pts',(19.337394846703,-21.4398735214983,3.20307054857503));
#145041=CARTESIAN_POINT('Ctrl Pts',(19.2543069264955,-21.4600251981986,
3.20732412646062));
#145042=CARTESIAN_POINT('Ctrl Pts',(19.1701138843276,-21.4760328992744,
3.21157770434621));
#145043=CARTESIAN_POINT('Ctrl Pts',(19.0852654759068,-21.4877863800873,
3.2158312822318));
#145044=CARTESIAN_POINT('Ctrl Pts',(19.0020620194665,-21.4993119967374,
3.22000239620914));
#145045=CARTESIAN_POINT('Ctrl Pts',(18.9182288577838,-21.5067468078097,
3.22417351018648));
#145046=CARTESIAN_POINT('Ctrl Pts',(18.8342009436325,-21.5100382661124,
3.22834462416382));
#145047=CARTESIAN_POINT('Ctrl Pts',(18.7502012258592,-21.5133286199344,
3.23251433848358));
#145048=CARTESIAN_POINT('Ctrl Pts',(18.6660073447033,-21.5124783642369,
3.23668405280334));
#145049=CARTESIAN_POINT('Ctrl Pts',(18.582057712998,-21.5074869480044,3.2408537671231));
#145050=CARTESIAN_POINT('Ctrl Pts',(18.4981110685809,-21.5024957093878,
3.24502333306653));
#145051=CARTESIAN_POINT('Ctrl Pts',(18.414409115505,-21.4933636313811,3.24919289900997));
#145052=CARTESIAN_POINT('Ctrl Pts',(18.3313872270487,-21.4801421943903,
3.2533624649534));
#145053=CARTESIAN_POINT('Ctrl Pts',(18.2454463913859,-21.4664559079809,
3.25767862769305));
#145054=CARTESIAN_POINT('Ctrl Pts',(18.1602348531239,-21.4483874314135,
3.2619947904327));
#145055=CARTESIAN_POINT('Ctrl Pts',(18.0762243702397,-21.4260515800794,
3.26631095317234));
#145056=CARTESIAN_POINT('Ctrl Pts',(17.9949505200244,-21.4044433167599,
3.27048651736342));
#145057=CARTESIAN_POINT('Ctrl Pts',(17.9148011124187,-21.378841616957,3.2746620815545));
#145058=CARTESIAN_POINT('Ctrl Pts',(17.8361862981299,-21.349400791844,3.27883764574558));
#145059=CARTESIAN_POINT('Ctrl Pts',(17.7536008364223,-21.3184729806292,
3.28322410775951));
#145060=CARTESIAN_POINT('Ctrl Pts',(17.6727096022459,-21.2833082561226,
3.28761056977344));
#145061=CARTESIAN_POINT('Ctrl Pts',(17.5939605452813,-21.2441409297172,
3.29199703178737));
#145062=CARTESIAN_POINT('Ctrl Pts',(17.5152114883168,-21.2049736033118,
3.2963834938013));
#145063=CARTESIAN_POINT('Ctrl Pts',(17.4386050767024,-21.161804026126,3.30076995581523));
#145064=CARTESIAN_POINT('Ctrl Pts',(17.364553744478,-21.1149186191895,3.30515641782916));
#145065=CARTESIAN_POINT('Ctrl Pts',(17.2939096238495,-21.070190479346,3.30934105222176));
#145066=CARTESIAN_POINT('Ctrl Pts',(17.2253276726157,-21.0219144506012,
3.31352568661436));
#145067=CARTESIAN_POINT('Ctrl Pts',(17.1591863942882,-20.97030674261,3.31771032100696));
#145068=CARTESIAN_POINT('Ctrl Pts',(17.093139259884,-20.9187724918035,3.32188899909045));
#145069=CARTESIAN_POINT('Ctrl Pts',(17.0295262575255,-20.8639162618917,
3.32606767717394));
#145070=CARTESIAN_POINT('Ctrl Pts',(16.9686982691563,-20.8059983276908,
3.33024635525743));
#145071=CARTESIAN_POINT('Ctrl Pts',(16.9067799828036,-20.7470422561362,
3.33449993314298));
#145072=CARTESIAN_POINT('Ctrl Pts',(16.8477479425957,-20.6849138964936,
3.33875351102853));
#145073=CARTESIAN_POINT('Ctrl Pts',(16.7919382910611,-20.6199317488055,
3.34300708891408));
#145074=CARTESIAN_POINT('Ctrl Pts',(16.7372106185328,-20.5562094068615,
3.34717820289155));
#145075=CARTESIAN_POINT('Ctrl Pts',(16.6855818186072,-20.4897433069906,
3.35134931686903));
#145076=CARTESIAN_POINT('Ctrl Pts',(16.6373315068437,-20.420870732844,3.35552043084651));
#145077=CARTESIAN_POINT('Ctrl Pts',(16.5890973859384,-20.352021269555,3.3596901451664));
#145078=CARTESIAN_POINT('Ctrl Pts',(16.544239765417,-20.2807673121879,3.36385985948629));
#145079=CARTESIAN_POINT('Ctrl Pts',(16.5029964131481,-20.207477198301,3.36802957380618));
#145080=CARTESIAN_POINT('Ctrl Pts',(16.4617545284946,-20.1341896923911,
3.37219913974973));
#145081=CARTESIAN_POINT('Ctrl Pts',(16.4241268812486,-20.0588665753509,
3.37636870569329));
#145082=CARTESIAN_POINT('Ctrl Pts',(16.3903058438335,-19.9819017925758,
3.38053827163684));
#145083=CARTESIAN_POINT('Ctrl Pts',(16.3552957004569,-19.9022310229649,
3.38485443437632));
#145084=CARTESIAN_POINT('Ctrl Pts',(16.3243650403573,-19.8208014806367,
3.3891705971158));
#145085=CARTESIAN_POINT('Ctrl Pts',(16.2976726756056,-19.7380719867858,
3.39348675985528));
#145086=CARTESIAN_POINT('Ctrl Pts',(16.2718498118347,-19.6580373975154,
3.39766232404646));
#145087=CARTESIAN_POINT('Ctrl Pts',(16.2499934356292,-19.5767867151056,
3.40183788823764));
#145088=CARTESIAN_POINT('Ctrl Pts',(16.2321958025117,-19.4947483371048,
3.40601345242882));
#145089=CARTESIAN_POINT('Ctrl Pts',(16.2134992532485,-19.4085663956273,
3.41039991444245));
#145090=CARTESIAN_POINT('Ctrl Pts',(16.1992823307861,-19.3215156705806,
3.41478637645608));
#145091=CARTESIAN_POINT('Ctrl Pts',(16.1895904829899,-19.2340996450696,
3.41917283846971));
#145092=CARTESIAN_POINT('Ctrl Pts',(16.1798986351937,-19.1466836195585,
3.42355930048334));
#145093=CARTESIAN_POINT('Ctrl Pts',(16.174731820223,-19.0589028772671,3.42794576249697));
#145094=CARTESIAN_POINT('Ctrl Pts',(16.1740724460423,-18.9712592442245,
3.43233222451059));
#145095=CARTESIAN_POINT('Ctrl Pts',(16.1740244495167,-18.9648795739235,
3.43265151959756));
#145096=CARTESIAN_POINT('Ctrl Pts',(16.1740003013853,-18.958499723977,3.43297081468453));
#145097=CARTESIAN_POINT('Ctrl Pts',(16.1740000028035,-18.9521198086917,
3.4332901097715));
#145098=CARTESIAN_POINT('',(16.1743944592445,-18.9523823947444,3.36670986511428));
#145099=CARTESIAN_POINT('Ctrl Pts',(20.293349366535,-20.9818838108338,3.08342410800431));
#145100=CARTESIAN_POINT('Ctrl Pts',(19.779330537192,-21.3686028835722,3.11541446101482));
#145101=CARTESIAN_POINT('Ctrl Pts',(18.2370602754448,-21.8303674869899,
3.18979674958582));
#145102=CARTESIAN_POINT('Ctrl Pts',(16.4590845454477,-20.6164716802603,
3.28422525531007));
#145103=CARTESIAN_POINT('Ctrl Pts',(16.1776267599649,-19.3569817996596,
3.34666340802382));
#145104=CARTESIAN_POINT('Ctrl Pts',(16.1781627867106,-18.9523866751972,
3.36670962517707));
#145105=CARTESIAN_POINT('Ctrl Pts',(16.1740000284928,-18.9523819467095,
3.3667098902285));
#145106=CARTESIAN_POINT('Ctrl Pts',(16.1739869935966,-18.8650154810558,
3.37103154303558));
#145107=CARTESIAN_POINT('Ctrl Pts',(16.1784506871914,-18.7777135371325,
3.37535319584266));
#145108=CARTESIAN_POINT('Ctrl Pts',(16.1873453738309,-18.6909440385447,
3.37967484864975));
#145109=CARTESIAN_POINT('Ctrl Pts',(16.1966194662204,-18.6004733587883,
3.38418084296216));
#145110=CARTESIAN_POINT('Ctrl Pts',(16.2107109130556,-18.5105820575904,
3.38868683727458));
#145111=CARTESIAN_POINT('Ctrl Pts',(16.2295088315793,-18.4217887333309,
3.39319283158699));
#145112=CARTESIAN_POINT('Ctrl Pts',(16.2475982064586,-18.3363422660913,
3.39752898296558));
#145113=CARTESIAN_POINT('Ctrl Pts',(16.2700454505065,-18.2519128648082,
3.40186513434417));
#145114=CARTESIAN_POINT('Ctrl Pts',(16.296700996459,-18.1689459997304,3.40620128572276));
#145115=CARTESIAN_POINT('Ctrl Pts',(16.3233900671469,-18.0858747870546,
3.41054289068792));
#145116=CARTESIAN_POINT('Ctrl Pts',(16.3542978445813,-18.0042701592832,
3.41488449565309));
#145117=CARTESIAN_POINT('Ctrl Pts',(16.3892268388776,-17.9245571437398,
3.41922610061825));
#145118=CARTESIAN_POINT('Ctrl Pts',(16.4242296046626,-17.8446757709924,
3.42357687523365));
#145119=CARTESIAN_POINT('Ctrl Pts',(16.4632703651625,-17.7666943545301,
3.42792764984905));
#145120=CARTESIAN_POINT('Ctrl Pts',(16.5061059491331,-17.6910130460184,
3.43227842446446));
#145121=CARTESIAN_POINT('Ctrl Pts',(16.5109248522389,-17.6824990756499,
3.43276787644255));
#145122=CARTESIAN_POINT('Ctrl Pts',(16.515791737601,-17.6740141830169,3.43325732842064));
#145123=CARTESIAN_POINT('Ctrl Pts',(16.5207062260025,-17.6655589131312,
3.43374678039873));
#145124=CARTESIAN_POINT('Ctrl Pts',(16.5627232942887,-17.5932694654538,
3.43793141479117));
#145125=CARTESIAN_POINT('Ctrl Pts',(16.608363899273,-17.5229061642045,3.44211604918361));
#145126=CARTESIAN_POINT('Ctrl Pts',(16.6574263400684,-17.4548554395523,
3.44630068357605));
#145127=CARTESIAN_POINT('Ctrl Pts',(16.7064189465521,-17.3869015766835,
3.4504793616594));
#145128=CARTESIAN_POINT('Ctrl Pts',(16.7588234476463,-17.3212541220954,
3.45465803974274));
#145129=CARTESIAN_POINT('Ctrl Pts',(16.8143930615577,-17.2582735752536,
3.45883671782609));
#145130=CARTESIAN_POINT('Ctrl Pts',(16.8709587208714,-17.1941641473616,
3.46309029571167));
#145131=CARTESIAN_POINT('Ctrl Pts',(16.930803836094,-17.1328185931037,3.46734387359726));
#145132=CARTESIAN_POINT('Ctrl Pts',(16.9936228831504,-17.0745848910946,
3.47159745148285));
#145133=CARTESIAN_POINT('Ctrl Pts',(17.0552240603871,-17.0174801630432,
3.47576856546019));
#145134=CARTESIAN_POINT('Ctrl Pts',(17.1196845346186,-16.9633680324694,
3.47993967943753));
#145135=CARTESIAN_POINT('Ctrl Pts',(17.1866778681086,-16.912540703971,3.48411079341487));
#145136=CARTESIAN_POINT('Ctrl Pts',(17.2536487213386,-16.8617304310735,
3.48828050773463));
#145137=CARTESIAN_POINT('Ctrl Pts',(17.3231503796754,-16.8142030489943,
3.49245022205439));
#145138=CARTESIAN_POINT('Ctrl Pts',(17.3948237869026,-16.7702101223367,
3.49661993637416));
#145139=CARTESIAN_POINT('Ctrl Pts',(17.4664946436824,-16.7262187611362,
3.50078950231759));
#145140=CARTESIAN_POINT('Ctrl Pts',(17.5403367031857,-16.6857618452163,
3.50495906826103));
#145141=CARTESIAN_POINT('Ctrl Pts',(17.6159635983346,-16.6490465474632,
3.50912863420446));
#145142=CARTESIAN_POINT('Ctrl Pts',(17.6942494418455,-16.6110403851225,
3.5134447969441));
#145143=CARTESIAN_POINT('Ctrl Pts',(17.7744474914057,-16.5770440773059,
3.51776095968374));
#145144=CARTESIAN_POINT('Ctrl Pts',(17.8561052781559,-16.5472337208456,
3.52207712242339));
#145145=CARTESIAN_POINT('Ctrl Pts',(17.9351030710671,-16.5183944336203,
3.52625268661447));
#145146=CARTESIAN_POINT('Ctrl Pts',(18.0154664958606,-16.4934726654686,
3.53042825080555));
#145147=CARTESIAN_POINT('Ctrl Pts',(18.0967709615458,-16.472576850848,3.53460381499663));
#145148=CARTESIAN_POINT('Ctrl Pts',(18.1821819225488,-16.450625638296,3.53899027701055));
#145149=CARTESIAN_POINT('Ctrl Pts',(18.2686309144569,-16.4331178853207,
3.54337673902447));
#145150=CARTESIAN_POINT('Ctrl Pts',(18.3556165397332,-16.4201180997139,
3.54776320103839));
#145151=CARTESIAN_POINT('Ctrl Pts',(18.4426021650095,-16.407118314107,3.55214966305232));
#145152=CARTESIAN_POINT('Ctrl Pts',(18.530123838803,-16.3986264761921,3.55653612506624));
#145153=CARTESIAN_POINT('Ctrl Pts',(18.6176794289204,-16.3946440363642,
3.56092258708016));
#145154=CARTESIAN_POINT('Ctrl Pts',(18.7012064565128,-16.3908448344978,
3.56510722147276));
#145155=CARTESIAN_POINT('Ctrl Pts',(18.7850752514674,-16.391135040087,3.56929185586537));
#145156=CARTESIAN_POINT('Ctrl Pts',(18.8688517103014,-16.3955542219267,
3.57347649025797));
#145157=CARTESIAN_POINT('Ctrl Pts',(18.9525089237155,-16.3999671136081,
3.57765516834146));
#145158=CARTESIAN_POINT('Ctrl Pts',(19.0360736066035,-16.4084972837709,
3.58183384642495));
#145159=CARTESIAN_POINT('Ctrl Pts',(19.1191090576612,-16.4211323595045,
3.58601252450843));
#145160=CARTESIAN_POINT('Ctrl Pts',(19.2036328595139,-16.4339939098916,
3.59026610239398));
#145161=CARTESIAN_POINT('Ctrl Pts',(19.2876077883166,-16.4511089960901,
3.59451968027953));
#145162=CARTESIAN_POINT('Ctrl Pts',(19.370575874736,-16.4724090749271,3.59877325816508));
#145163=CARTESIAN_POINT('Ctrl Pts',(19.4519354628899,-16.4932962101692,
3.60294437214256));
#145164=CARTESIAN_POINT('Ctrl Pts',(19.5323264333864,-16.5182073979463,
3.60711548612004));
#145165=CARTESIAN_POINT('Ctrl Pts',(19.6113263938458,-16.5470263205886,
3.61128660009752));
#145166=CARTESIAN_POINT('Ctrl Pts',(19.6902998451053,-16.575835572763,3.61545631441741));
#145167=CARTESIAN_POINT('Ctrl Pts',(19.7678827815192,-16.6085497980588,
3.6196260287373));
#145168=CARTESIAN_POINT('Ctrl Pts',(19.8436693267471,-16.6450032541686,
3.62379574305719));
#145169=CARTESIAN_POINT('Ctrl Pts',(19.9194531751644,-16.6814554131079,
3.62796530900075));
#145170=CARTESIAN_POINT('Ctrl Pts',(19.993440345293,-16.7216463381321,3.6321348749443));
#145171=CARTESIAN_POINT('Ctrl Pts',(20.06524750435,-16.7653632944264,3.63630444088786));
#145172=CARTESIAN_POINT('Ctrl Pts',(20.139579314554,-16.8106172849844,3.64062060362734));
#145173=CARTESIAN_POINT('Ctrl Pts',(20.2115745125432,-16.8596495964176,
3.64493676636682));
#145174=CARTESIAN_POINT('Ctrl Pts',(20.2808401159382,-16.9121750918953,
3.6492529291063));
#145175=CARTESIAN_POINT('Ctrl Pts',(20.3478493995713,-16.9629895748699,
3.65342849329748));
#145176=CARTESIAN_POINT('Ctrl Pts',(20.4123038602611,-17.0170728169147,
3.65760405748865));
#145177=CARTESIAN_POINT('Ctrl Pts',(20.4738824987383,-17.074126497715,3.66177962167983));
#145178=CARTESIAN_POINT('Ctrl Pts',(20.5385713278796,-17.1340618243223,
3.66616608369346));
#145179=CARTESIAN_POINT('Ctrl Pts',(20.6000857771511,-17.1972751310407,
3.67055254570709));
#145180=CARTESIAN_POINT('Ctrl Pts',(20.6581002087316,-17.2633797387337,
3.67493900772071));
#145181=CARTESIAN_POINT('Ctrl Pts',(20.716114640312,-17.3294843464266,3.67932546973434));
#145182=CARTESIAN_POINT('Ctrl Pts',(20.7706287541777,-17.3984797526766,
3.68371193174797));
#145183=CARTESIAN_POINT('Ctrl Pts',(20.8213695361432,-17.4699445288447,
3.6880983937616));
#145184=CARTESIAN_POINT('Ctrl Pts',(20.8697756595073,-17.5381211047148,
3.69228302815506));
#145185=CARTESIAN_POINT('Ctrl Pts',(20.914928230553,-17.6087985715452,3.69646766254852));
#145186=CARTESIAN_POINT('Ctrl Pts',(20.956559006204,-17.6816333348432,3.70065229694198));
#145187=CARTESIAN_POINT('Ctrl Pts',(20.9981305255987,-17.7543644268708,
3.70483097502633));
#145188=CARTESIAN_POINT('Ctrl Pts',(21.0361899803433,-17.8292463201213,
3.70900965311069));
#145189=CARTESIAN_POINT('Ctrl Pts',(21.0705113959643,-17.905905120685,3.71318833119505));
#145190=CARTESIAN_POINT('Ctrl Pts',(21.1054479982896,-17.9839379751455,
3.71744190908038));
#145191=CARTESIAN_POINT('Ctrl Pts',(21.1365109555626,-18.0638116724909,
3.72169548696571));
#145192=CARTESIAN_POINT('Ctrl Pts',(21.1635100116305,-18.1451040318682,
3.72594906485105));
#145193=CARTESIAN_POINT('Ctrl Pts',(21.1899856383155,-18.22482038024,3.73012017882942));
#145194=CARTESIAN_POINT('Ctrl Pts',(21.2125533792703,-18.3059004177639,
3.7342912928078));
#145195=CARTESIAN_POINT('Ctrl Pts',(21.2310824062636,-18.3879260187451,
3.73846240678618));
#145196=CARTESIAN_POINT('Ctrl Pts',(21.249605215663,-18.4699240952438,3.74263212110699));
#145197=CARTESIAN_POINT('Ctrl Pts',(21.2640919013283,-18.5528666566977,
3.74680183542779));
#145198=CARTESIAN_POINT('Ctrl Pts',(21.2744621331457,-18.6363227121685,
3.75097154974859));
#145199=CARTESIAN_POINT('Ctrl Pts',(21.2848319959458,-18.7197757979147,
3.75514111569307));
#145200=CARTESIAN_POINT('Ctrl Pts',(21.2910856402585,-18.8037418847205,
3.75931068163754));
#145201=CARTESIAN_POINT('Ctrl Pts',(21.293194451632,-18.887783501059,3.76348024758202));
#145202=CARTESIAN_POINT('Ctrl Pts',(21.2953774062114,-18.9747799169322,
3.76779641032044));
#145203=CARTESIAN_POINT('Ctrl Pts',(21.293118626995,-19.0618567451373,3.77211257305885));
#145204=CARTESIAN_POINT('Ctrl Pts',(21.2864451550249,-19.148529210526,3.77642873579727));
#145205=CARTESIAN_POINT('Ctrl Pts',(21.2799890707009,-19.2323783294898,
3.7806042999894));
#145206=CARTESIAN_POINT('Ctrl Pts',(21.2694016000863,-19.315848563955,3.78477986418152));
#145207=CARTESIAN_POINT('Ctrl Pts',(21.2547598325396,-19.3985085292071,
3.78895542837364));
#145208=CARTESIAN_POINT('Ctrl Pts',(21.2393785441267,-19.4853434527702,
3.79334189038521));
#145209=CARTESIAN_POINT('Ctrl Pts',(21.21952276158,-19.5712835336821,3.79772835239677));
#145210=CARTESIAN_POINT('Ctrl Pts',(21.1953413592831,-19.6558456599869,
3.80211481440834));
#145211=CARTESIAN_POINT('Ctrl Pts',(21.1711599569862,-19.7404077862916,
3.8065012764199));
#145212=CARTESIAN_POINT('Ctrl Pts',(21.1426531949957,-19.8235914337676,
3.81088773843147));
#145213=CARTESIAN_POINT('Ctrl Pts',(21.1100276507034,-19.9049389293616,
3.81527420044303));
#145214=CARTESIAN_POINT('Ctrl Pts',(21.0789046619559,-19.982540000698,3.81945864581518));
#145215=CARTESIAN_POINT('Ctrl Pts',(21.0439180829632,-20.0587591592275,
3.82364309118733));
#145216=CARTESIAN_POINT('Ctrl Pts',(21.0052116068261,-20.1331849292209,
3.82782753655948));
#145217=CARTESIAN_POINT('Ctrl Pts',(20.966557925707,-20.2075091836474,3.83200627441467));
#145218=CARTESIAN_POINT('Ctrl Pts',(20.9241946333094,-20.2800445023936,
3.83618501226986));
#145219=CARTESIAN_POINT('Ctrl Pts',(20.8783138059628,-20.3503984773867,
3.84036375012505));
#145220=CARTESIAN_POINT('Ctrl Pts',(20.8324875829267,-20.4206687217558,
3.84453751472425));
#145221=CARTESIAN_POINT('Ctrl Pts',(20.7831523972177,-20.4887624000407,
3.84871127932344));
#145222=CARTESIAN_POINT('Ctrl Pts',(20.7305459075014,-20.5543122165294,
3.85288504392264));
#145223=CARTESIAN_POINT('Ctrl Pts',(20.6779756656207,-20.6198168667471,
3.85705593264219));
#145224=CARTESIAN_POINT('Ctrl Pts',(20.622138884113,-20.6827807791786,3.86122682136175));
#145225=CARTESIAN_POINT('Ctrl Pts',(20.5633154981063,-20.7428670549173,
3.8653977100813));
#145226=CARTESIAN_POINT('Ctrl Pts',(20.5045103316162,-20.8029347199814,
3.86956730694091));
#145227=CARTESIAN_POINT('Ctrl Pts',(20.4427207177839,-20.8601261886896,
3.87373690380052));
#145228=CARTESIAN_POINT('Ctrl Pts',(20.3782648488349,-20.914139930506,3.87790650066013));
#145229=CARTESIAN_POINT('Ctrl Pts',(20.3505067188033,-20.9374011244559,
3.87970215113689));
#145230=CARTESIAN_POINT('Ctrl Pts',(20.3222545566491,-20.960073441674,3.88149780161365));
#145231=CARTESIAN_POINT('Ctrl Pts',(20.2935357468249,-20.9821350335323,
3.88329345209042));
#145232=CARTESIAN_POINT('Origin',(18.734,-18.952,-1.76670989022851));
#145233=CARTESIAN_POINT('',(20.2917778074115,-20.9798105030549,4.74997346711436));
#145234=CARTESIAN_POINT('',(20.2944552458115,-20.9833106134465,4.68319930664559));
#145235=CARTESIAN_POINT('',(20.2935357468249,-20.9821350335323,-1.76670989022851));
#145236=CARTESIAN_POINT('',(16.1740009581142,-18.9542148462772,4.23329008724971));
#145237=CARTESIAN_POINT('Ctrl Pts',(16.1756127776244,-18.9542129983521,
4.2332901097715));
#145238=CARTESIAN_POINT('Ctrl Pts',(16.1805387770827,-18.3551144017957,
4.26304769694121));
#145239=CARTESIAN_POINT('Ctrl Pts',(16.6895187238437,-16.8950156783259,
4.3351972196714));
#145240=CARTESIAN_POINT('Ctrl Pts',(19.1239734419868,-15.950132033759,4.44973867796206));
#145241=CARTESIAN_POINT('Ctrl Pts',(21.4691811314196,-17.6550517548787,
4.5769144846435));
#145242=CARTESIAN_POINT('Ctrl Pts',(21.3400058517746,-19.9330438229453,
4.67699274769427));
#145243=CARTESIAN_POINT('Ctrl Pts',(20.5375803711221,-20.7936897955478,
4.73467907518456));
#145244=CARTESIAN_POINT('Ctrl Pts',(20.2917778074114,-20.979810503055,4.74997346711437));
#145245=CARTESIAN_POINT('Ctrl Pts',(20.2935357468249,-20.9821350335323,
3.94993168858525));
#145246=CARTESIAN_POINT('Ctrl Pts',(20.2271357439777,-21.033143058279,3.95411195890108));
#145247=CARTESIAN_POINT('Ctrl Pts',(20.1581247303567,-21.080971361085,3.95829222921691));
#145248=CARTESIAN_POINT('Ctrl Pts',(20.0868406859495,-21.1253435251795,
3.96247249953274));
#145249=CARTESIAN_POINT('Ctrl Pts',(20.0156413709827,-21.1696629477571,
3.96664780110743));
#145250=CARTESIAN_POINT('Ctrl Pts',(19.9421747810589,-21.210534151495,3.97082310268211));
#145251=CARTESIAN_POINT('Ctrl Pts',(19.8668100196579,-21.2477224264625,
3.9749984042568));
#145252=CARTESIAN_POINT('Ctrl Pts',(19.7915083980674,-21.2848795454813,
3.97917020780741));
#145253=CARTESIAN_POINT('Ctrl Pts',(19.7143121762206,-21.3183596641629,
3.98334201135802));
#145254=CARTESIAN_POINT('Ctrl Pts',(19.6356162179364,-21.3479733294747,
3.98751381490862));
#145255=CARTESIAN_POINT('Ctrl Pts',(19.5569539985136,-21.3775742986917,
3.99168382990611));
#145256=CARTESIAN_POINT('Ctrl Pts',(19.4767937494083,-21.4033119443507,
3.9958538449036));
#145257=CARTESIAN_POINT('Ctrl Pts',(19.395550402454,-21.4250448974924,4.00002385990109));
#145258=CARTESIAN_POINT('Ctrl Pts',(19.3143175153553,-21.4467750525765,
4.0041933380207));
#145259=CARTESIAN_POINT('Ctrl Pts',(19.232002251929,-21.4645014211188,4.00836281614032));
#145260=CARTESIAN_POINT('Ctrl Pts',(19.1490334747512,-21.4781328577167,
4.01253229425994));
#145261=CARTESIAN_POINT('Ctrl Pts',(19.0660504912852,-21.4917666283507,
4.01670248629641));
#145262=CARTESIAN_POINT('Ctrl Pts',(18.9824142259904,-21.5013040015176,
4.02087267833288));
#145263=CARTESIAN_POINT('Ctrl Pts',(18.8985611115136,-21.5067053921299,
4.02504287036935));
#145264=CARTESIAN_POINT('Ctrl Pts',(18.814615568438,-21.5121127365218,4.02921765907475));
#145265=CARTESIAN_POINT('Ctrl Pts',(18.7304531589254,-21.5133749701138,
4.03339244778016));
#145266=CARTESIAN_POINT('Ctrl Pts',(18.6465122350704,-21.5105046200833,
4.03756723648557));
#145267=CARTESIAN_POINT('Ctrl Pts',(18.5625187387461,-21.5076324723434,
4.04174463987451));
#145268=CARTESIAN_POINT('Ctrl Pts',(18.4787474622756,-21.5006226277578,
4.04592204326345));
#145269=CARTESIAN_POINT('Ctrl Pts',(18.395631157065,-21.4895394629701,4.05009944665238));
#145270=CARTESIAN_POINT('Ctrl Pts',(18.3123782833495,-21.4784380874206,
4.05428371393804));
#145271=CARTESIAN_POINT('Ctrl Pts',(18.229782980652,-21.4632501162163,4.0584679812237));
#145272=CARTESIAN_POINT('Ctrl Pts',(18.1482669036117,-21.4440908369872,
4.06265224850936));
#145273=CARTESIAN_POINT('Ctrl Pts',(18.1121675017119,-21.4356061484924,
4.0645052516455));
#145274=CARTESIAN_POINT('Ctrl Pts',(18.076279539388,-21.4263432749685,4.06635825478164));
#145275=CARTESIAN_POINT('Ctrl Pts',(18.0406384682269,-21.4163152773655,
4.06821125791777));
#145276=CARTESIAN_POINT('Ctrl Pts',(17.9601502870268,-21.3936690643915,
4.07239589231081));
#145277=CARTESIAN_POINT('Ctrl Pts',(17.8806229756134,-21.3670332665356,
4.07658052670385));
#145278=CARTESIAN_POINT('Ctrl Pts',(17.8024810747699,-21.3365067607239,
4.08076516109689));
#145279=CARTESIAN_POINT('Ctrl Pts',(17.7244503992504,-21.306023705615,4.08494383918082));
#145280=CARTESIAN_POINT('Ctrl Pts',(17.6478016421986,-21.2716611086066,
4.08912251726475));
#145281=CARTESIAN_POINT('Ctrl Pts',(17.5729454850813,-21.2335679725546,
4.09330119534867));
#145282=CARTESIAN_POINT('Ctrl Pts',(17.4967475851455,-21.1947920444157,
4.09755477323411));
#145283=CARTESIAN_POINT('Ctrl Pts',(17.422407646075,-21.1521506525344,4.10180835111955));
#145284=CARTESIAN_POINT('Ctrl Pts',(17.3503388850133,-21.1058528080799,
4.10606192900499));
#145285=CARTESIAN_POINT('Ctrl Pts',(17.2796673175155,-21.0604525376831,
4.11023304298293));
#145286=CARTESIAN_POINT('Ctrl Pts',(17.2111800563182,-21.0115365845697,
4.11440415696087));
#145287=CARTESIAN_POINT('Ctrl Pts',(17.1452415288503,-20.959348131329,4.11857527093882));
#145288=CARTESIAN_POINT('Ctrl Pts',(17.0793251276922,-20.9071771904278,
4.12274498525918));
#145289=CARTESIAN_POINT('Ctrl Pts',(17.01595612214,-20.8517362155439,4.12691469957954));
#145290=CARTESIAN_POINT('Ctrl Pts',(16.9554677262149,-20.7933101181237,
4.1310844138999));
#145291=CARTESIAN_POINT('Ctrl Pts',(16.8949814827263,-20.7348860997546,
4.13525397984395));
#145292=CARTESIAN_POINT('Ctrl Pts',(16.8373759753517,-20.6734774902646,
4.139423545788));
#145293=CARTESIAN_POINT('Ctrl Pts',(16.7829482470746,-20.6094067266084,
4.14359311173204));
#145294=CARTESIAN_POINT('Ctrl Pts',(16.7266069070151,-20.5430833139417,
4.14790927447097));
#145295=CARTESIAN_POINT('Ctrl Pts',(16.6736713066581,-20.47390746331,4.1522254372099));
#145296=CARTESIAN_POINT('Ctrl Pts',(16.6244248933205,-20.4022733774286,
4.15654159994883));
#145297=CARTESIAN_POINT('Ctrl Pts',(16.5767826767178,-20.3329727643605,
4.1607171641405));
#145298=CARTESIAN_POINT('Ctrl Pts',(16.5325931948253,-20.2613720362608,
4.16489272833218));
#145299=CARTESIAN_POINT('Ctrl Pts',(16.4920674161606,-20.1878552866412,
4.16906829252386));
#145300=CARTESIAN_POINT('Ctrl Pts',(16.4494947767562,-20.1106253807675,
4.17345475453641));
#145301=CARTESIAN_POINT('Ctrl Pts',(16.4109659295264,-20.0312813353545,
4.17784121654897));
#145302=CARTESIAN_POINT('Ctrl Pts',(16.3766684749372,-19.9502925828358,
4.18222767856152));
#145303=CARTESIAN_POINT('Ctrl Pts',(16.342371020348,-19.8693038303171,4.18661414057408));
#145304=CARTESIAN_POINT('Ctrl Pts',(16.3123050853067,-19.7866709419478,
4.19100060258663));
#145305=CARTESIAN_POINT('Ctrl Pts',(16.2865973915759,-19.702879798822,4.19538706459919));
#145306=CARTESIAN_POINT('Ctrl Pts',(16.2566341527394,-19.6052182170345,
4.2004996433589));
#145307=CARTESIAN_POINT('Ctrl Pts',(16.2324986213406,-19.5056900725379,
4.20561222211862));
#145308=CARTESIAN_POINT('Ctrl Pts',(16.2143850329185,-19.404924295726,4.21072480087833));
#145309=CARTESIAN_POINT('Ctrl Pts',(16.1965183144937,-19.3055318551339,
4.21576770033015));
#145310=CARTESIAN_POINT('Ctrl Pts',(16.1845105456257,-19.2049352741343,
4.22081059978196));
#145311=CARTESIAN_POINT('Ctrl Pts',(16.1785021632643,-19.1037590407164,
4.22585349923378));
#145312=CARTESIAN_POINT('Ctrl Pts',(16.1755487125963,-19.0540253526453,
4.22833236190576));
#145313=CARTESIAN_POINT('Ctrl Pts',(16.174044162412,-19.0041519285503,4.23081122457773));
#145314=CARTESIAN_POINT('Ctrl Pts',(16.1740009581142,-18.9542148462772,
4.23329008724971));
#145315=CARTESIAN_POINT('',(16.1740010840393,-18.9496440968074,4.16670989022851));
#145316=CARTESIAN_POINT('Ctrl Pts',(20.2935357468249,-20.9821350335323,
3.88329345209042));
#145317=CARTESIAN_POINT('Ctrl Pts',(20.2268447907951,-21.0333665665094,
3.88746332012199));
#145318=CARTESIAN_POINT('Ctrl Pts',(20.1576354539796,-21.081301703658,3.89163318815356));
#145319=CARTESIAN_POINT('Ctrl Pts',(20.0862723557994,-21.1256971904432,
3.89580305618514));
#145320=CARTESIAN_POINT('Ctrl Pts',(20.0148340605621,-21.1701394578481,
3.89997731810953));
#145321=CARTESIAN_POINT('Ctrl Pts',(19.9412378639014,-21.2110343840631,
3.90415158003392));
#145322=CARTESIAN_POINT('Ctrl Pts',(19.8658750790502,-21.2481835304316,
3.90832584195832));
#145323=CARTESIAN_POINT('Ctrl Pts',(19.7904707301851,-21.2853531652631,
3.91250240606781));
#145324=CARTESIAN_POINT('Ctrl Pts',(19.7132982754322,-21.318772723907,3.9166789701773));
#145325=CARTESIAN_POINT('Ctrl Pts',(19.6347689672755,-21.348291982959,3.92085553428679));
#145326=CARTESIAN_POINT('Ctrl Pts',(19.5561040322652,-21.3778622243043,
3.92503931168088));
#145327=CARTESIAN_POINT('Ctrl Pts',(19.4760780019455,-21.4035185719984,
3.92922308907496));
#145328=CARTESIAN_POINT('Ctrl Pts',(19.3951169987244,-21.425160794206,3.93340686646905));
#145329=CARTESIAN_POINT('Ctrl Pts',(19.3367852034137,-21.440753852909,3.93642124668752));
#145330=CARTESIAN_POINT('Ctrl Pts',(19.2779683413532,-21.4542642055276,
3.939435626906));
#145331=CARTESIAN_POINT('Ctrl Pts',(19.2188278686569,-21.4656710082613,
3.94245000712447));
#145332=CARTESIAN_POINT('Ctrl Pts',(19.1367276562992,-21.4815062034173,
3.94663464151748));
#145333=CARTESIAN_POINT('Ctrl Pts',(19.0536980417282,-21.4933443659488,
3.95081927591048));
#145334=CARTESIAN_POINT('Ctrl Pts',(18.9701628470243,-21.5010835823263,
3.95500391030349));
#145335=CARTESIAN_POINT('Ctrl Pts',(18.8867465543307,-21.5088117828872,
3.95918258838737));
#145336=CARTESIAN_POINT('Ctrl Pts',(18.8028265650705,-21.5124525840587,
3.96336126647126));
#145337=CARTESIAN_POINT('Ctrl Pts',(18.7188367813175,-21.511955092731,3.96753994455515));
#145338=CARTESIAN_POINT('Ctrl Pts',(18.6333415410516,-21.5114486842287,
3.97179352244059));
#145339=CARTESIAN_POINT('Ctrl Pts',(18.5477744529633,-21.5066540748902,
3.97604710032604));
#145340=CARTESIAN_POINT('Ctrl Pts',(18.4625985845178,-21.4975728769128,
3.98030067821149));
#145341=CARTESIAN_POINT('Ctrl Pts',(18.3790740164904,-21.4886677356789,
3.98447179218939));
#145342=CARTESIAN_POINT('Ctrl Pts',(18.2959261128669,-21.4756407813848,
3.98864290616729));
#145343=CARTESIAN_POINT('Ctrl Pts',(18.2135896449266,-21.4585460423324,
3.99281402014519));
#145344=CARTESIAN_POINT('Ctrl Pts',(18.1312808057834,-21.4414570395849,
3.99698373446551));
#145345=CARTESIAN_POINT('Ctrl Pts',(18.0497833116132,-21.4203030564001,
4.00115344878582));
#145346=CARTESIAN_POINT('Ctrl Pts',(17.9695227367358,-21.39518941426,4.00532316310613));
#145347=CARTESIAN_POINT('Ctrl Pts',(17.8892650178741,-21.370076665771,4.00949272905012));
#145348=CARTESIAN_POINT('Ctrl Pts',(17.8102445695797,-21.3410046766655,
4.0136622949941));
#145349=CARTESIAN_POINT('Ctrl Pts',(17.7328714533957,-21.3081285264548,
4.01783186093808));
#145350=CARTESIAN_POINT('Ctrl Pts',(17.6527779938943,-21.2740964913587,
4.02214802367707));
#145351=CARTESIAN_POINT('Ctrl Pts',(17.574450347639,-21.2359880155545,4.02646418641605));
#145352=CARTESIAN_POINT('Ctrl Pts',(17.4983185919004,-21.1940284248147,
4.03078034915504));
#145353=CARTESIAN_POINT('Ctrl Pts',(17.4246668200994,-21.153435663331,4.03495591334666));
#145354=CARTESIAN_POINT('Ctrl Pts',(17.3530704495486,-21.1092391216323,
4.03913147753829));
#145355=CARTESIAN_POINT('Ctrl Pts',(17.283890236673,-21.0616875774161,4.04330704172991));
#145356=CARTESIAN_POINT('Ctrl Pts',(17.2112158957024,-21.0117343177425,
4.04769350374258));
#145357=CARTESIAN_POINT('Ctrl Pts',(17.1412086706277,-20.9580785813379,
4.05207996575524));
#145358=CARTESIAN_POINT('Ctrl Pts',(17.0742466821567,-20.9010559057934,
4.05646642776791));
#145359=CARTESIAN_POINT('Ctrl Pts',(17.0072846936857,-20.8440332302489,
4.06085288978057));
#145360=CARTESIAN_POINT('Ctrl Pts',(16.943368311327,-20.7836440693278,4.06523935179323));
#145361=CARTESIAN_POINT('Ctrl Pts',(16.8828286089282,-20.7202659530956,
4.0696258138059));
#145362=CARTESIAN_POINT('Ctrl Pts',(16.8258191500137,-20.66058359639,4.07375648865202));
#145363=CARTESIAN_POINT('Ctrl Pts',(16.7715797255597,-20.5980163329693,
4.07788716349815));
#145364=CARTESIAN_POINT('Ctrl Pts',(16.720421868205,-20.5328551822216,4.08201783834428));
#145365=CARTESIAN_POINT('Ctrl Pts',(16.6693300782615,-20.467778183328,4.08614317866297));
#145366=CARTESIAN_POINT('Ctrl Pts',(16.6213122506322,-20.4001143092104,
4.09026851898165));
#145367=CARTESIAN_POINT('Ctrl Pts',(16.5766430483355,-20.3301911997632,
4.09439385930034));
#145368=CARTESIAN_POINT('Ctrl Pts',(16.5320173182039,-20.2603361396388,
4.09851518482882));
#145369=CARTESIAN_POINT('Ctrl Pts',(16.4907340001793,-20.1882266026471,
4.1026365103573));
#145370=CARTESIAN_POINT('Ctrl Pts',(16.4530264539488,-20.1142218730582,
4.10675783588578));
#145371=CARTESIAN_POINT('Ctrl Pts',(16.4153436115611,-20.0402656271648,
4.11087646135585));
#145372=CARTESIAN_POINT('Ctrl Pts',(16.3812321043791,-19.9644170734852,
4.11499508682592));
#145373=CARTESIAN_POINT('Ctrl Pts',(16.3508802454214,-19.8870616211443,
4.11911371229599));
#145374=CARTESIAN_POINT('Ctrl Pts',(16.3205285952527,-19.8097067009281,
4.12323230943423));
#145375=CARTESIAN_POINT('Ctrl Pts',(16.2939367323083,-19.7308453355426,
4.12735090657246));
#145376=CARTESIAN_POINT('Ctrl Pts',(16.2712450678812,-19.6508834983921,
4.13146950371069));
#145377=CARTESIAN_POINT('Ctrl Pts',(16.2485547151173,-19.570926283335,4.1355878627786));
#145378=CARTESIAN_POINT('Ctrl Pts',(16.2297642345971,-19.4898691801182,
4.1397062218465));
#145379=CARTESIAN_POINT('Ctrl Pts',(16.2149637529308,-19.4081319830394,
4.14382458091441));
#145380=CARTESIAN_POINT('Ctrl Pts',(16.2001500672816,-19.3263218655941,
4.14794661410208));
#145381=CARTESIAN_POINT('Ctrl Pts',(16.1893335672674,-19.2438309098088,
4.15206864728976));
#145382=CARTESIAN_POINT('Ctrl Pts',(16.1825528364004,-19.1610869947166,
4.15619068047744));
#145383=CARTESIAN_POINT('Ctrl Pts',(16.1767848147302,-19.0907009692733,
4.1596970837278));
#145384=CARTESIAN_POINT('Ctrl Pts',(16.1739362156169,-19.020132176051,4.16320348697815));
#145385=CARTESIAN_POINT('Ctrl Pts',(16.1740010840393,-18.9496440968074,
4.16670989022851));
#145386=CARTESIAN_POINT('Ctrl Pts',(16.174088184599,-18.9496434116999,4.16670992829755));
#145387=CARTESIAN_POINT('Ctrl Pts',(16.1722334877636,-18.748007243103,4.17674049236081));
#145388=CARTESIAN_POINT('Ctrl Pts',(16.2862273000593,-17.6962739531831,
4.22916299198455));
#145389=CARTESIAN_POINT('Ctrl Pts',(17.7370129389085,-16.0937997547996,
4.32397742716877));
#145390=CARTESIAN_POINT('Ctrl Pts',(20.5976438994044,-16.5666020755754,
4.4511532338502));
#145391=CARTESIAN_POINT('Ctrl Pts',(21.6812139993619,-19.0722717640235,
4.57089386034247));
#145392=CARTESIAN_POINT('Ctrl Pts',(20.8466207859578,-20.5504284027622,
4.64824255127427));
#145393=CARTESIAN_POINT('Ctrl Pts',(20.2944552458116,-20.9833106134464,
4.68319930664559));
#145394=CARTESIAN_POINT('Origin',(18.734,-18.952,-1.76670989022851));
#145395=CARTESIAN_POINT('',(20.2935357468249,-20.9821350335323,5.54983331705304));
#145396=CARTESIAN_POINT('',(20.2935357468249,-20.9821350335323,5.4833696516309));
#145397=CARTESIAN_POINT('',(20.2935357468249,-20.9821350335323,-1.76670989022851));
#145398=CARTESIAN_POINT('',(16.1741505039397,-18.9508032548666,5.03329016024815));
#145399=CARTESIAN_POINT('Ctrl Pts',(16.1740002797795,-18.9508031412289,
5.03329016239971));
#145400=CARTESIAN_POINT('Ctrl Pts',(16.1740435234788,-18.8583078019676,
5.03786858507912));
#145401=CARTESIAN_POINT('Ctrl Pts',(16.1791038614083,-18.7659792628304,
5.04244700775854));
#145402=CARTESIAN_POINT('Ctrl Pts',(16.1891023385012,-18.6743385289637,
5.04702543043795));
#145403=CARTESIAN_POINT('Ctrl Pts',(16.1991318881351,-18.5824130006799,
5.05161808160685));
#145404=CARTESIAN_POINT('Ctrl Pts',(16.2141301908472,-18.4911798450087,
5.05621073277575));
#145405=CARTESIAN_POINT('Ctrl Pts',(16.2339673694791,-18.401148979913,5.06080338394464));
#145406=CARTESIAN_POINT('Ctrl Pts',(16.253896242195,-18.3107019620039,5.06541726388551));
#145407=CARTESIAN_POINT('Ctrl Pts',(16.2787086950666,-18.2214686541854,
5.07003114382637));
#145408=CARTESIAN_POINT('Ctrl Pts',(16.3082244096464,-18.1339457320907,
5.07464502376723));
#145409=CARTESIAN_POINT('Ctrl Pts',(16.3316224115872,-18.064563657823,5.07830258630123));
#145410=CARTESIAN_POINT('Ctrl Pts',(16.3579750606108,-17.996256071474,5.08196014883524));
#145411=CARTESIAN_POINT('Ctrl Pts',(16.3871718743356,-17.9292596866308,
5.08561771136924));
#145412=CARTESIAN_POINT('Ctrl Pts',(16.4205760854036,-17.8526088095457,
5.08980234576229));
#145413=CARTESIAN_POINT('Ctrl Pts',(16.4578017058021,-17.7774535557437,
5.09398698015534));
#145414=CARTESIAN_POINT('Ctrl Pts',(16.4986929228155,-17.7042010295369,
5.09817161454839));
#145415=CARTESIAN_POINT('Ctrl Pts',(16.5395259362428,-17.6310527692343,
5.10235029263233));
#145416=CARTESIAN_POINT('Ctrl Pts',(16.5840139603303,-17.559802255246,5.10652897071626));
#145417=CARTESIAN_POINT('Ctrl Pts',(16.6319534129312,-17.4908360304906,
5.1107076488002));
#145418=CARTESIAN_POINT('Ctrl Pts',(16.6807521457665,-17.4206336357216,
5.11496122668564));
#145419=CARTESIAN_POINT('Ctrl Pts',(16.7331270652481,-17.3527986694292,
5.11921480457108));
#145420=CARTESIAN_POINT('Ctrl Pts',(16.7888147952352,-17.2877120083459,
5.12346838245651));
#145421=CARTESIAN_POINT('Ctrl Pts',(16.8434229099109,-17.2238871791938,
5.12763949643446));
#145422=CARTESIAN_POINT('Ctrl Pts',(16.9012162179242,-17.1627054093257,
5.13181061041241));
#145423=CARTESIAN_POINT('Ctrl Pts',(16.961904139826,-17.1044945839446,5.13598172439036));
#145424=CARTESIAN_POINT('Ctrl Pts',(17.0225716973095,-17.0463032917681,
5.14015143871074));
#145425=CARTESIAN_POINT('Ctrl Pts',(17.086131607912,-16.9910812823427,5.14432115303111));
#145426=CARTESIAN_POINT('Ctrl Pts',(17.1522562065725,-16.9391198316955,
5.14849086735148));
#145427=CARTESIAN_POINT('Ctrl Pts',(17.218378452236,-16.8871602300597,5.15266043329552));
#145428=CARTESIAN_POINT('Ctrl Pts',(17.2870648422621,-16.8384612400851,
5.15682999923956));
#145429=CARTESIAN_POINT('Ctrl Pts',(17.3579554657567,-16.7932731901004,
5.1609995651836));
#145430=CARTESIAN_POINT('Ctrl Pts',(17.4313385161205,-16.7464963840237,
5.16531572792253));
#145431=CARTESIAN_POINT('Ctrl Pts',(17.5070832408523,-16.7034822843462,
5.16963189066145));
#145432=CARTESIAN_POINT('Ctrl Pts',(17.5847604857694,-16.6644579700187,
5.17394805340037));
#145433=CARTESIAN_POINT('Ctrl Pts',(17.6599074026034,-16.6267048686259,
5.17812361759205));
#145434=CARTESIAN_POINT('Ctrl Pts',(17.7368624194976,-16.5926857570979,
5.18229918178373));
#145435=CARTESIAN_POINT('Ctrl Pts',(17.81521627489,-16.5625572895604,5.1864747459754));
#145436=CARTESIAN_POINT('Ctrl Pts',(17.8975275972497,-16.5309071047512,
5.19086120798795));
#145437=CARTESIAN_POINT('Ctrl Pts',(17.9813822273942,-16.5035511069692,
5.19524767000049));
#145438=CARTESIAN_POINT('Ctrl Pts',(18.0662895457778,-16.4806111699446,
5.19963413201304));
#145439=CARTESIAN_POINT('Ctrl Pts',(18.1511968641614,-16.4576712329201,
5.20402059402558));
#145440=CARTESIAN_POINT('Ctrl Pts',(18.2371562875636,-16.439147404523,5.20840705603812));
#145441=CARTESIAN_POINT('Ctrl Pts',(18.3236691980734,-16.4250990060965,
5.21279351805067));
#145442=CARTESIAN_POINT('Ctrl Pts',(18.4062015213278,-16.4116969953064,
5.21697815244372));
#145443=CARTESIAN_POINT('Ctrl Pts',(18.4895447184805,-16.4023177375285,
5.22116278683677));
#145444=CARTESIAN_POINT('Ctrl Pts',(18.573272140763,-16.3970505767697,5.22534742122982));
#145445=CARTESIAN_POINT('Ctrl Pts',(18.6568803874232,-16.3917909131622,
5.22952609931376));
#145446=CARTESIAN_POINT('Ctrl Pts',(18.7408713177055,-16.3906317491884,
5.2337047773977));
#145447=CARTESIAN_POINT('Ctrl Pts',(18.8248097150325,-16.3936111328307,
5.23788345548165));
#145448=CARTESIAN_POINT('Ctrl Pts',(18.910252647806,-16.3966439197836,5.24213703336708));
#145449=CARTESIAN_POINT('Ctrl Pts',(18.9956406698882,-16.4039651578947,
5.24639061125252));
#145450=CARTESIAN_POINT('Ctrl Pts',(19.0805109637125,-16.4155595508613,
5.25064418913795));
#145451=CARTESIAN_POINT('Ctrl Pts',(19.1637358812804,-16.4269291638956,
5.25481530311591));
#145452=CARTESIAN_POINT('Ctrl Pts',(19.2464624890054,-16.44240765832,5.25898641709386));
#145453=CARTESIAN_POINT('Ctrl Pts',(19.3282578021761,-16.4619281808444,
5.26315753107181));
#145454=CARTESIAN_POINT('Ctrl Pts',(19.4100256681395,-16.4814421530689,
5.26732724539218));
#145455=CARTESIAN_POINT('Ctrl Pts',(19.4908624130939,-16.504995352978,5.27149695971256));
#145456=CARTESIAN_POINT('Ctrl Pts',(19.570345761113,-16.5324699282984,5.27566667403293));
#145457=CARTESIAN_POINT('Ctrl Pts',(19.6498262807736,-16.5599435259555,
5.27983623997698));
#145458=CARTESIAN_POINT('Ctrl Pts',(19.7279530647408,-16.5913380704867,
5.28400580592102));
#145459=CARTESIAN_POINT('Ctrl Pts',(19.8043208135647,-16.6264864317639,
5.28817537186507));
#145460=CARTESIAN_POINT('Ctrl Pts',(19.8833735582274,-16.6628705660633,
5.29249153460399));
#145461=CARTESIAN_POINT('Ctrl Pts',(19.9605407918123,-16.7032771763716,
5.29680769734291));
#145462=CARTESIAN_POINT('Ctrl Pts',(20.0353992838381,-16.7474683254656,
5.30112386008183));
#145463=CARTESIAN_POINT('Ctrl Pts',(20.10781926836,-16.7902199525259,5.30529942427351));
#145464=CARTESIAN_POINT('Ctrl Pts',(20.1780782485914,-16.8365130434918,
5.30947498846519));
#145465=CARTESIAN_POINT('Ctrl Pts',(20.2458229776825,-16.8860882680639,
5.31365055265687));
#145466=CARTESIAN_POINT('Ctrl Pts',(20.3169893319923,-16.9381674193753,
5.31803701466941));
#145467=CARTESIAN_POINT('Ctrl Pts',(20.3853803178148,-16.993868610292,5.32242347668195));
#145468=CARTESIAN_POINT('Ctrl Pts',(20.450627895575,-17.052845275357,5.32680993869449));
#145469=CARTESIAN_POINT('Ctrl Pts',(20.5158754733353,-17.1118219404221,
5.33119640070703));
#145470=CARTESIAN_POINT('Ctrl Pts',(20.5779792870959,-17.1740736151504,
5.33558286271957));
#145471=CARTESIAN_POINT('Ctrl Pts',(20.6366195645771,-17.239213150305,5.33996932473211));
#145472=CARTESIAN_POINT('Ctrl Pts',(20.6925617159657,-17.3013555188871,
5.34415395912515));
#145473=CARTESIAN_POINT('Ctrl Pts',(20.7455602793472,-17.3663571440021,
5.3483385935182));
#145474=CARTESIAN_POINT('Ctrl Pts',(20.7953091936645,-17.4339076417707,
5.35252322791125));
#145475=CARTESIAN_POINT('Ctrl Pts',(20.8449872965599,-17.5013619897667,
5.35670190599519));
#145476=CARTESIAN_POINT('Ctrl Pts',(20.891424667568,-17.5713576368075,5.36088058407914));
#145477=CARTESIAN_POINT('Ctrl Pts',(20.934353739878,-17.6435492292772,5.36505926216308));
#145478=CARTESIAN_POINT('Ctrl Pts',(20.9780522849565,-17.7170348041588,
5.36931284004852));
#145479=CARTESIAN_POINT('Ctrl Pts',(21.0181151991572,-17.7927954651137,
5.37356641793395));
#145480=CARTESIAN_POINT('Ctrl Pts',(21.0543048298795,-17.8704337762125,
5.37781999581939));
#145481=CARTESIAN_POINT('Ctrl Pts',(21.089792853992,-17.9465669171521,5.38199110979734));
#145482=CARTESIAN_POINT('Ctrl Pts',(21.1215562334332,-18.0245051179383,
5.38616222377529));
#145483=CARTESIAN_POINT('Ctrl Pts',(21.1494168148284,-18.1038481205324,
5.39033333775324));
#145484=CARTESIAN_POINT('Ctrl Pts',(21.1772680473364,-18.1831644988156,
5.39450305207362));
#145485=CARTESIAN_POINT('Ctrl Pts',(21.2012189304412,-18.2638843090191,
5.39867276639399));
#145486=CARTESIAN_POINT('Ctrl Pts',(21.2211399893044,-18.3455886927151,
5.40284248071436));
#145487=CARTESIAN_POINT('Ctrl Pts',(21.2410603392908,-18.4272901690185,
5.4070120466584));
#145488=CARTESIAN_POINT('Ctrl Pts',(21.2569510420042,-18.5099757020134,
5.41118161260245));
#145489=CARTESIAN_POINT('Ctrl Pts',(21.2687332465284,-18.5932140346339,
5.41535117854649));
#145490=CARTESIAN_POINT('Ctrl Pts',(21.2809296988287,-18.6793789243437,
5.41966734128541));
#145491=CARTESIAN_POINT('Ctrl Pts',(21.2887232939913,-18.766135687597,5.42398350402433));
#145492=CARTESIAN_POINT('Ctrl Pts',(21.2920850129342,-18.8529996636307,
5.42829966676325));
#145493=CARTESIAN_POINT('Ctrl Pts',(21.2953372242362,-18.9370340547816,
5.43247523095493));
#145494=CARTESIAN_POINT('Ctrl Pts',(21.2944419142066,-19.0211683105535,
5.43665079514661));
#145495=CARTESIAN_POINT('Ctrl Pts',(21.2894259327675,-19.1049650356757,
5.44082635933829));
#145496=CARTESIAN_POINT('Ctrl Pts',(21.2841566060303,-19.1929941341762,
5.44521282135083));
#145497=CARTESIAN_POINT('Ctrl Pts',(21.2743394628619,-19.2806501283313,
5.44959928336337));
#145498=CARTESIAN_POINT('Ctrl Pts',(21.2600666971253,-19.3674359657934,
5.45398574537591));
#145499=CARTESIAN_POINT('Ctrl Pts',(21.2457939313886,-19.4542218032555,
5.45837220738845));
#145500=CARTESIAN_POINT('Ctrl Pts',(21.2270657409798,-19.5401369333207,
5.46275866940099));
#145501=CARTESIAN_POINT('Ctrl Pts',(21.2040345704695,-19.6247029215675,
5.46714513141354));
#145502=CARTESIAN_POINT('Ctrl Pts',(21.1820669712701,-19.7053636823778,
5.4713290281613));
#145503=CARTESIAN_POINT('Ctrl Pts',(21.1561032921522,-19.7850973400373,
5.47551292490906));
#145504=CARTESIAN_POINT('Ctrl Pts',(21.1262387968713,-19.8634787648343,
5.47969682165682));
#145505=CARTESIAN_POINT('Ctrl Pts',(21.0964141293845,-19.9417556588425,
5.48387513868938));
#145506=CARTESIAN_POINT('Ctrl Pts',(21.0626991366584,-20.0186834745666,
5.48805345572194));
#145507=CARTESIAN_POINT('Ctrl Pts',(21.0252393289067,-20.0938504007405,
5.4922317727545));
#145508=CARTESIAN_POINT('Ctrl Pts',(20.9878182356716,-20.1689396422868,
5.49640577151812));
#145509=CARTESIAN_POINT('Ctrl Pts',(20.9466602184249,-20.2422711993806,
5.50057977028174));
#145510=CARTESIAN_POINT('Ctrl Pts',(20.9019590364997,-20.3134527593932,
5.50475376904535));
#145511=CARTESIAN_POINT('Ctrl Pts',(20.8572882174555,-20.3845859699629,
5.50892493265736));
#145512=CARTESIAN_POINT('Ctrl Pts',(20.809079257669,-20.4535716954205,5.51309609626937));
#145513=CARTESIAN_POINT('Ctrl Pts',(20.7575714330065,-20.5200429380346,
5.51726725988138));
#145514=CARTESIAN_POINT('Ctrl Pts',(20.7060846236983,-20.5864870601728,
5.52143672164553));
#145515=CARTESIAN_POINT('Ctrl Pts',(20.6513019074181,-20.65041837625,5.52560618340968));
#145516=CARTESIAN_POINT('Ctrl Pts',(20.5935045656375,-20.7115007162185,
5.52977564517383));
#145517=CARTESIAN_POINT('Ctrl Pts',(20.5356974931368,-20.7725933399669,
5.53394580890565));
#145518=CARTESIAN_POINT('Ctrl Pts',(20.4748750940648,-20.8308356918434,
5.53811597263746));
#145519=CARTESIAN_POINT('Ctrl Pts',(20.4113567585225,-20.885927171493,5.54228613636927));
#145520=CARTESIAN_POINT('Ctrl Pts',(20.3730381707404,-20.9191621056419,
5.54480186326386));
#145521=CARTESIAN_POINT('Ctrl Pts',(20.3337391579018,-20.951251050111,5.54731759015845));
#145522=CARTESIAN_POINT('Ctrl Pts',(20.2935357468249,-20.9821350335323,
5.54983331705304));
#145523=CARTESIAN_POINT('Ctrl Pts',(20.2917778074114,-20.979810503055,4.74997346711437));
#145524=CARTESIAN_POINT('Ctrl Pts',(19.8562818605801,-21.3095662733656,
4.77707101074504));
#145525=CARTESIAN_POINT('Ctrl Pts',(18.4733993847563,-21.8166034507402,
4.84656048993618));
#145526=CARTESIAN_POINT('Ctrl Pts',(16.5671405548292,-20.815635979695,4.94099937082189));
#145527=CARTESIAN_POINT('Ctrl Pts',(16.1797898378084,-19.4541224957223,
5.00834070807693));
#145528=CARTESIAN_POINT('Ctrl Pts',(16.1776748285763,-18.9508059208577,
5.0332901097715));
#145529=CARTESIAN_POINT('',(16.1737368696253,-18.9528355653615,4.96670989022851));
#145530=CARTESIAN_POINT('Ctrl Pts',(20.2944552458116,-20.9833106134464,
4.68319930664559));
#145531=CARTESIAN_POINT('Ctrl Pts',(20.1770115574137,-21.0753831528721,
4.69063448683475));
#145532=CARTESIAN_POINT('Ctrl Pts',(19.3369083430137,-21.6211180130261,
4.74046160258439));
#145533=CARTESIAN_POINT('Ctrl Pts',(17.2348043616254,-21.581772666889,4.8326806538945));
#145534=CARTESIAN_POINT('Ctrl Pts',(16.1917618388527,-19.8928505847622,
4.91974900156632));
#145535=CARTESIAN_POINT('Ctrl Pts',(16.1699049957539,-18.998574246681,4.96442541367765));
#145536=CARTESIAN_POINT('Ctrl Pts',(16.1700997034774,-18.952836752384,4.96670989022851));
#145537=CARTESIAN_POINT('Ctrl Pts',(16.1740001363332,-18.952835479442,4.96670989022851));
#145538=CARTESIAN_POINT('Ctrl Pts',(16.1739730621524,-18.8698772454868,
4.97085977152528));
#145539=CARTESIAN_POINT('Ctrl Pts',(16.1779827035226,-18.7867551328103,
4.97500965282205));
#145540=CARTESIAN_POINT('Ctrl Pts',(16.1860506816107,-18.7038986680416,
4.97915953411883));
#145541=CARTESIAN_POINT('Ctrl Pts',(16.194107496698,-18.6211568449803,4.98330367356457));
#145542=CARTESIAN_POINT('Ctrl Pts',(16.2062114544436,-18.5386804021303,
4.98744781301032));
#145543=CARTESIAN_POINT('Ctrl Pts',(16.2223321624274,-18.4568993297282,
4.99159195245607));
#145544=CARTESIAN_POINT('Ctrl Pts',(16.2384354396283,-18.3752066844675,
4.99573161098228));
#145545=CARTESIAN_POINT('Ctrl Pts',(16.258546748188,-18.2942083730103,4.99987126950849));
#145546=CARTESIAN_POINT('Ctrl Pts',(16.2825840079951,-18.2143282341429,
5.0040109280347));
#145547=CARTESIAN_POINT('Ctrl Pts',(16.3066073287289,-18.1344944173239,
5.00814818599595));
#145548=CARTESIAN_POINT('Ctrl Pts',(16.33455194816,-18.0557779336924,5.0122854439572));
#145549=CARTESIAN_POINT('Ctrl Pts',(16.3662852025775,-17.9785902003439,
5.01642270191845));
#145550=CARTESIAN_POINT('Ctrl Pts',(16.3980099615293,-17.9014231313034,
5.020558852274));
#145551=CARTESIAN_POINT('Ctrl Pts',(16.4335211635118,-17.8257844328042,
5.02469500262956));
#145552=CARTESIAN_POINT('Ctrl Pts',(16.4726375176037,-17.7520667838541,
5.02883115298511));
#145553=CARTESIAN_POINT('Ctrl Pts',(16.5117556109323,-17.6783458571842,
5.03296748724699));
#145554=CARTESIAN_POINT('Ctrl Pts',(16.5544789534253,-17.6065465624547,
5.03710382150887));
#145555=CARTESIAN_POINT('Ctrl Pts',(16.6005803897996,-17.5370368319944,
5.04124015577075));
#145556=CARTESIAN_POINT('Ctrl Pts',(16.646728500548,-17.4674567279532,5.04538067777228));
#145557=CARTESIAN_POINT('Ctrl Pts',(16.6962612737695,-17.4001712070013,
5.04952119977381));
#145558=CARTESIAN_POINT('Ctrl Pts',(16.7489086678727,-17.3355185113609,
5.05366172177533));
#145559=CARTESIAN_POINT('Ctrl Pts',(16.8015842228024,-17.2708312333184,
5.05780445852127));
#145560=CARTESIAN_POINT('Ctrl Pts',(16.8573774008556,-17.2087799314012,
5.06194719526721));
#145561=CARTESIAN_POINT('Ctrl Pts',(16.9159800655235,-17.1496672011401,
5.06608993201314));
#145562=CARTESIAN_POINT('Ctrl Pts',(16.9746826938398,-17.0904536371675,
5.07023973538449));
#145563=CARTESIAN_POINT('Ctrl Pts',(17.0362040315237,-17.0341889688223,
5.07438953875584));
#145564=CARTESIAN_POINT('Ctrl Pts',(17.1002018437186,-16.9811363353769,
5.07853934212719));
#145565=CARTESIAN_POINT('Ctrl Pts',(17.1438608301676,-16.9449440949669,
5.08137031717058));
#145566=CARTESIAN_POINT('Ctrl Pts',(17.1886716656529,-16.910245843732,5.08420129221397));
#145567=CARTESIAN_POINT('Ctrl Pts',(17.2345184376715,-16.8771132454428,
5.08703226725736));
#145568=CARTESIAN_POINT('Ctrl Pts',(17.302287307428,-16.8281379601765,5.09121690165041));
#145569=CARTESIAN_POINT('Ctrl Pts',(17.3725842232475,-16.78239517261,5.09540153604346));
#145570=CARTESIAN_POINT('Ctrl Pts',(17.4450678487465,-16.7401559934152,
5.09958617043651));
#145571=CARTESIAN_POINT('Ctrl Pts',(17.5174483027761,-16.6979769364639,
5.10376484852044));
#145572=CARTESIAN_POINT('Ctrl Pts',(17.5920088899902,-16.6592918118672,
5.10794352660438));
#145573=CARTESIAN_POINT('Ctrl Pts',(17.668377621725,-16.6243297168801,5.11212220468832));
#145574=CARTESIAN_POINT('Ctrl Pts',(17.7461152080912,-16.588740951467,5.11637578257375));
#145575=CARTESIAN_POINT('Ctrl Pts',(17.8257260077699,-16.5570102814917,
5.12062936045919));
#145576=CARTESIAN_POINT('Ctrl Pts',(17.9067894477687,-16.5293314914588,
5.12488293834462));
#145577=CARTESIAN_POINT('Ctrl Pts',(17.9862813148007,-16.5021893087815,
5.12905405232258));
#145578=CARTESIAN_POINT('Ctrl Pts',(18.0671695448446,-16.4789434563412,
5.13322516630053));
#145579=CARTESIAN_POINT('Ctrl Pts',(18.1490371223199,-16.4597282588497,
5.13739628027848));
#145580=CARTESIAN_POINT('Ctrl Pts',(18.230877228339,-16.4405195092033,5.14156599459885));
#145581=CARTESIAN_POINT('Ctrl Pts',(18.3136955816366,-16.4253388333998,
5.14573570891923));
#145582=CARTESIAN_POINT('Ctrl Pts',(18.3970618790066,-16.4142701675274,
5.1499054232396));
#145583=CARTESIAN_POINT('Ctrl Pts',(18.4804252098459,-16.4032018955257,
5.15407498918364));
#145584=CARTESIAN_POINT('Ctrl Pts',(18.5643359898469,-16.3962454022306,
5.15824455512768));
#145585=CARTESIAN_POINT('Ctrl Pts',(18.6483570024146,-16.3934329641449,
5.16241412107172));
#145586=CARTESIAN_POINT('Ctrl Pts',(18.7353320901331,-16.3905216442056,
5.16673028381064));
#145587=CARTESIAN_POINT('Ctrl Pts',(18.8224247790685,-16.3920512290412,
5.17104644654956));
#145588=CARTESIAN_POINT('Ctrl Pts',(18.9091500846456,-16.3979987376964,
5.17536260928849));
#145589=CARTESIAN_POINT('Ctrl Pts',(18.9930503225153,-16.4037525068826,
5.17953817348017));
#145590=CARTESIAN_POINT('Ctrl Pts',(19.0766062822584,-16.4136406900188,
5.18371373767185));
#145591=CARTESIAN_POINT('Ctrl Pts',(19.1593859487955,-16.4275898125369,
5.18788930186352));
#145592=CARTESIAN_POINT('Ctrl Pts',(19.2463466194995,-16.4422434720725,
5.19227576387607));
#145593=CARTESIAN_POINT('Ctrl Pts',(19.3324499449359,-16.4613789616178,
5.19666222588862));
#145594=CARTESIAN_POINT('Ctrl Pts',(19.4172115835231,-16.4848514572203,
5.20104868790117));
#145595=CARTESIAN_POINT('Ctrl Pts',(19.5019732221102,-16.5083239528228,
5.20543514991371));
#145596=CARTESIAN_POINT('Ctrl Pts',(19.5853926474676,-16.5361331988246,
5.20982161192626));
#145597=CARTESIAN_POINT('Ctrl Pts',(19.6670104728637,-16.5680764572817,
5.21420807393881));
#145598=CARTESIAN_POINT('Ctrl Pts',(19.7448729411266,-16.5985499590658,
5.21839270833186));
#145599=CARTESIAN_POINT('Ctrl Pts',(19.8213857737637,-16.6328988372128,
5.22257734272491));
#145600=CARTESIAN_POINT('Ctrl Pts',(19.8961362506934,-16.6709828289063,
5.22676197711796));
#145601=CARTESIAN_POINT('Ctrl Pts',(19.9707803295716,-16.7090126127515,
5.23094065520191));
#145602=CARTESIAN_POINT('Ctrl Pts',(20.0436666290096,-16.7507667429072,
5.23511933328585));
#145603=CARTESIAN_POINT('Ctrl Pts',(20.1144011640629,-16.7960564417746,
5.2392980113698));
#145604=CARTESIAN_POINT('Ctrl Pts',(20.186403564821,-16.842157925945,5.24355158925524));
#145605=CARTESIAN_POINT('Ctrl Pts',(20.2561758527108,-16.8919227999547,
5.24780516714067));
#145606=CARTESIAN_POINT('Ctrl Pts',(20.3233274374464,-16.9451023203511,
5.25205874502611));
#145607=CARTESIAN_POINT('Ctrl Pts',(20.3891771576765,-16.9972508519734,
5.25622985900406));
#145608=CARTESIAN_POINT('Ctrl Pts',(20.4525065055991,-17.052682513567,5.26040097298202));
#145609=CARTESIAN_POINT('Ctrl Pts',(20.5129768127645,-17.1111193684417,
5.26457208695997));
#145610=CARTESIAN_POINT('Ctrl Pts',(20.5734268285343,-17.1695366142654,
5.26874180128035));
#145611=CARTESIAN_POINT('Ctrl Pts',(20.6310193783568,-17.2309567312121,
5.27291151560072));
#145612=CARTESIAN_POINT('Ctrl Pts',(20.6854509703006,-17.2950633353948,
5.2770812299211));
#145613=CARTESIAN_POINT('Ctrl Pts',(20.7398806253347,-17.3591676583894,
5.28125079586514));
#145614=CARTESIAN_POINT('Ctrl Pts',(20.7911492490277,-17.4259579273212,
5.28542036180918));
#145615=CARTESIAN_POINT('Ctrl Pts',(20.838993044898,-17.4950839828834,5.28958992775322));
#145616=CARTESIAN_POINT('Ctrl Pts',(20.8885189696096,-17.566640425283,5.29390609049214));
#145617=CARTESIAN_POINT('Ctrl Pts',(20.934374451502,-17.6406995292214,5.29822225323106));
#145618=CARTESIAN_POINT('Ctrl Pts',(20.9763163009699,-17.7168410602662,
5.30253841596997));
#145619=CARTESIAN_POINT('Ctrl Pts',(21.016891899103,-17.7905022889458,5.30671398016165));
#145620=CARTESIAN_POINT('Ctrl Pts',(21.0538047581692,-17.8661119140599,
5.31088954435333));
#145621=CARTESIAN_POINT('Ctrl Pts',(21.0868828170839,-17.9432669089043,
5.31506510854501));
#145622=CARTESIAN_POINT('Ctrl Pts',(21.1216315701187,-18.0243188191198,
5.31945157055755));
#145623=CARTESIAN_POINT('Ctrl Pts',(21.1521477486479,-18.1070757672225,
5.32383803257009));
#145624=CARTESIAN_POINT('Ctrl Pts',(21.1782909617847,-18.1910521081326,
5.32822449458263));
#145625=CARTESIAN_POINT('Ctrl Pts',(21.2044341749215,-18.2750284490427,
5.33261095659517));
#145626=CARTESIAN_POINT('Ctrl Pts',(21.226204352714,-18.3602236017744,5.3369974186077));
#145627=CARTESIAN_POINT('Ctrl Pts',(21.2435233083642,-18.4461415565825,
5.34138388062024));
#145628=CARTESIAN_POINT('Ctrl Pts',(21.2600453931922,-18.528106298929,5.34556851501329));
#145629=CARTESIAN_POINT('Ctrl Pts',(21.2725783676242,-18.6110338790214,
5.34975314940634));
#145630=CARTESIAN_POINT('Ctrl Pts',(21.2810167729394,-18.6945013429835,
5.35393778379939));
#145631=CARTESIAN_POINT('Ctrl Pts',(21.2894431672291,-18.7778500013417,
5.35811646188332));
#145632=CARTESIAN_POINT('Ctrl Pts',(21.2937865229904,-18.8617365633854,
5.36229513996726));
#145633=CARTESIAN_POINT('Ctrl Pts',(21.293992315731,-18.945727568392,5.36647381805119));
#145634=CARTESIAN_POINT('Ctrl Pts',(21.2942017971586,-19.0312240518003,
5.37072739593663));
#145635=CARTESIAN_POINT('Ctrl Pts',(21.2901238296771,-19.1168282866476,
5.37498097382207));
#145636=CARTESIAN_POINT('Ctrl Pts',(21.2817561480521,-19.2020772082028,
5.37923455170751));
#145637=CARTESIAN_POINT('Ctrl Pts',(21.2735506902637,-19.2856734130641,
5.38340566568545));
#145638=CARTESIAN_POINT('Ctrl Pts',(21.2612204100085,-19.3689274796563,
5.3875767796634));
#145639=CARTESIAN_POINT('Ctrl Pts',(21.2448156932503,-19.4514041995498,
5.39174789364135));
#145640=CARTESIAN_POINT('Ctrl Pts',(21.2284164812532,-19.5338532435835,
5.39591760796173));
#145641=CARTESIAN_POINT('Ctrl Pts',(21.2079456377351,-19.6155250081441,
5.4000873222821));
#145642=CARTESIAN_POINT('Ctrl Pts',(21.1835049170499,-19.6959930519489,
5.40425703660247));
#145643=CARTESIAN_POINT('Ctrl Pts',(21.1590650660705,-19.7764582323552,
5.40842660254651));
#145644=CARTESIAN_POINT('Ctrl Pts',(21.1306557533067,-19.8557193372406,
5.41259616849056));
#145645=CARTESIAN_POINT('Ctrl Pts',(21.0984286192897,-19.9333650209193,
5.4167657344346));
#145646=CARTESIAN_POINT('Ctrl Pts',(21.065068418997,-20.0137406310499,5.42108189717352));
#145647=CARTESIAN_POINT('Ctrl Pts',(21.0276171353225,-20.092384622854,5.42539805991244));
#145648=CARTESIAN_POINT('Ctrl Pts',(20.9862964849993,-20.1688650474313,
5.42971422265136));
#145649=CARTESIAN_POINT('Ctrl Pts',(20.9463218505143,-20.2428541302222,
5.43388978684304));
#145650=CARTESIAN_POINT('Ctrl Pts',(20.9027263517807,-20.3148180591345,
5.43806535103473));
#145651=CARTESIAN_POINT('Ctrl Pts',(20.8557557370747,-20.3843940073146,
5.44224091522641));
#145652=CARTESIAN_POINT('Ctrl Pts',(20.8064127482818,-20.4574840712362,
5.44662737723895));
#145653=CARTESIAN_POINT('Ctrl Pts',(20.7533450801511,-20.5279381144878,
5.4510138392515));
#145654=CARTESIAN_POINT('Ctrl Pts',(20.6968850924154,-20.5953752200801,
5.45540030126404));
#145655=CARTESIAN_POINT('Ctrl Pts',(20.6404251046797,-20.6628123256725,
5.45978676327659));
#145656=CARTESIAN_POINT('Ctrl Pts',(20.5805732479924,-20.7272321203105,
5.46417322528913));
#145657=CARTESIAN_POINT('Ctrl Pts',(20.5177042670233,-20.788300380603,5.46855968730168));
#145658=CARTESIAN_POINT('Ctrl Pts',(20.4577251723804,-20.8465615279495,
5.47274451766067));
#145659=CARTESIAN_POINT('Ctrl Pts',(20.3947769753923,-20.9019893649409,
5.47692934801966));
#145660=CARTESIAN_POINT('Ctrl Pts',(20.3291582734039,-20.9542662367405,
5.48111417837865));
#145661=CARTESIAN_POINT('Ctrl Pts',(20.3173695655801,-20.9636580221449,
5.48186600279606));
#145662=CARTESIAN_POINT('Ctrl Pts',(20.3054947684578,-20.9729481955016,
5.48261782721348));
#145663=CARTESIAN_POINT('Ctrl Pts',(20.2935357468249,-20.9821350335323,
5.4833696516309));
#145664=CARTESIAN_POINT('Origin',(18.734,-18.952,-1.76670989022851));
#145665=CARTESIAN_POINT('',(20.2958869033725,-20.9851650055234,6.34984102531927));
#145666=CARTESIAN_POINT('',(20.2935357468249,-20.9821350335323,6.2833427999391));
#145667=CARTESIAN_POINT('',(20.2935357468249,-20.9821350335323,-1.76670989022851));
#145668=CARTESIAN_POINT('',(16.1740005630998,-18.9503020392334,5.8332901097715));
#145669=CARTESIAN_POINT('Ctrl Pts',(16.1712326851452,-18.9503002033939,
5.8332901097715));
#145670=CARTESIAN_POINT('Ctrl Pts',(16.1704460832798,-18.847523176255,5.83841759033362));
#145671=CARTESIAN_POINT('Ctrl Pts',(16.2227680109981,-17.8958349863275,
5.88593700645621));
#145672=CARTESIAN_POINT('Ctrl Pts',(17.4141948925089,-16.2277744127114,
5.97584835813928));
#145673=CARTESIAN_POINT('Ctrl Pts',(20.3102571282625,-16.3676811269119,
6.10302416482071));
#145674=CARTESIAN_POINT('Ctrl Pts',(21.731566457484,-18.8289532658523,6.22768838721405));
#145675=CARTESIAN_POINT('Ctrl Pts',(20.9266954653819,-20.4955799071986,
6.3099606740469));
#145676=CARTESIAN_POINT('Ctrl Pts',(20.2958869033725,-20.9851650055234,
6.34984102531927));
#145677=CARTESIAN_POINT('Ctrl Pts',(20.2935357468249,-20.9821350335323,
5.54983331705304));
#145678=CARTESIAN_POINT('Ctrl Pts',(20.2268225019857,-21.0333836886193,
5.55400789577091));
#145679=CARTESIAN_POINT('Ctrl Pts',(20.157617582879,-21.0813119452572,5.55818247448878));
#145680=CARTESIAN_POINT('Ctrl Pts',(20.0862916035558,-21.12568521616,5.56235705320665));
#145681=CARTESIAN_POINT('Ctrl Pts',(20.0149229753758,-21.1700850197413,
5.56653412808387));
#145682=CARTESIAN_POINT('Ctrl Pts',(19.9414311643003,-21.2109253827401,
5.57071120296108));
#145683=CARTESIAN_POINT('Ctrl Pts',(19.8662111471552,-21.2480178392725,
5.5748882778383));
#145684=CARTESIAN_POINT('Ctrl Pts',(19.7908651826575,-21.2851724028993,
5.57907234675171));
#145685=CARTESIAN_POINT('Ctrl Pts',(19.7137856568982,-21.3185663488317,
5.58325641566512));
#145686=CARTESIAN_POINT('Ctrl Pts',(19.6353869037669,-21.3480596089658,
5.58744048457852));
#145687=CARTESIAN_POINT('Ctrl Pts',(19.5924128683777,-21.3642262487927,
5.58973396908401));
#145688=CARTESIAN_POINT('Ctrl Pts',(19.5490427171948,-21.3792217476382,
5.5920274535895));
#145689=CARTESIAN_POINT('Ctrl Pts',(19.5053461655913,-21.393029514944,5.59432093809498));
#145690=CARTESIAN_POINT('Ctrl Pts',(19.4256185318269,-21.4182228213827,
5.59850557248803));
#145691=CARTESIAN_POINT('Ctrl Pts',(19.3445069543659,-21.4395528703719,
5.60269020688108));
#145692=CARTESIAN_POINT('Ctrl Pts',(19.2624206826503,-21.4568695738795,
5.60687484127413));
#145693=CARTESIAN_POINT('Ctrl Pts',(19.1804512505824,-21.4741616292031,
5.61105351935807));
#145694=CARTESIAN_POINT('Ctrl Pts',(19.0975103262626,-21.4874515917235,
5.61523219744201));
#145695=CARTESIAN_POINT('Ctrl Pts',(19.0140230530431,-21.4966388918203,
5.61941087552596));
#145696=CARTESIAN_POINT('Ctrl Pts',(18.9290393304524,-21.5059908676686,
5.62366445341139));
#145697=CARTESIAN_POINT('Ctrl Pts',(18.8434899394336,-21.511091508697,5.62791803129683));
#145698=CARTESIAN_POINT('Ctrl Pts',(18.7578350465905,-21.5118890387191,
5.63217160918226));
#145699=CARTESIAN_POINT('Ctrl Pts',(18.6738407409869,-21.5126711070654,
5.63634272316022));
#145700=CARTESIAN_POINT('Ctrl Pts',(18.5897454689696,-21.5093154194064,
5.64051383713817));
#145701=CARTESIAN_POINT('Ctrl Pts',(18.5059873315595,-21.5018255279589,
5.64468495111612));
#145702=CARTESIAN_POINT('Ctrl Pts',(18.4222573000012,-21.4943381498168,
5.64885466543649));
#145703=CARTESIAN_POINT('Ctrl Pts',(18.3388646361978,-21.4827193639703,
5.65302437975686));
#145704=CARTESIAN_POINT('Ctrl Pts',(18.2562442180635,-21.4670247340387,
5.65719409407724));
#145705=CARTESIAN_POINT('Ctrl Pts',(18.1736267399183,-21.4513306625893,
5.66136366002128));
#145706=CARTESIAN_POINT('Ctrl Pts',(18.091781904597,-21.4315611221137,5.66553322596532));
#145707=CARTESIAN_POINT('Ctrl Pts',(18.0111349162339,-21.4078228907378,
5.66970279190937));
#145708=CARTESIAN_POINT('Ctrl Pts',(17.9276524792488,-21.383250052431,5.67401895464829));
#145709=CARTESIAN_POINT('Ctrl Pts',(17.8454541950082,-21.3544244012909,
5.67833511738721));
#145710=CARTESIAN_POINT('Ctrl Pts',(17.7649932472175,-21.3215201862533,
5.68265128012613));
#145711=CARTESIAN_POINT('Ctrl Pts',(17.687153306338,-21.2896878225596,5.68682684431781));
#145712=CARTESIAN_POINT('Ctrl Pts',(17.6109396593039,-21.2540387751657,
5.69100240850949));
#145713=CARTESIAN_POINT('Ctrl Pts',(17.5367393343474,-21.2147785791988,
5.69517797270117));
#145714=CARTESIAN_POINT('Ctrl Pts',(17.4587913273718,-21.1735354440659,
5.69956443471371));
#145715=CARTESIAN_POINT('Ctrl Pts',(17.3830658746253,-21.1283070744552,
5.70395089672625));
#145716=CARTESIAN_POINT('Ctrl Pts',(17.3099772536614,-21.0793831854911,
5.70833735873879));
#145717=CARTESIAN_POINT('Ctrl Pts',(17.2368886326976,-21.030459296527,5.71272382075133));
#145718=CARTESIAN_POINT('Ctrl Pts',(17.166437262867,-20.9778402963549,5.71711028276386));
#145719=CARTESIAN_POINT('Ctrl Pts',(17.0989955289256,-20.9218630357379,
5.72149674477641));
#145720=CARTESIAN_POINT('Ctrl Pts',(17.0355419517776,-20.8691959820086,
5.72562381401755));
#145721=CARTESIAN_POINT('Ctrl Pts',(16.9745020021859,-20.8133485129554,
5.72975088325869));
#145722=CARTESIAN_POINT('Ctrl Pts',(16.9162185170907,-20.7545732940416,
5.73387795249984));
#145723=CARTESIAN_POINT('Ctrl Pts',(16.8577217299027,-20.6955829734197,
5.73802012571949));
#145724=CARTESIAN_POINT('Ctrl Pts',(16.8020020379165,-20.6336436795684,
5.74216229893914));
#145725=CARTESIAN_POINT('Ctrl Pts',(16.7493744028763,-20.5690532580101,
5.7463044721588));
#145726=CARTESIAN_POINT('Ctrl Pts',(16.6970742796337,-20.5048647949489,
5.75042086784547));
#145727=CARTESIAN_POINT('Ctrl Pts',(16.6478281605157,-20.4380584608901,
5.75453726353214));
#145728=CARTESIAN_POINT('Ctrl Pts',(16.6019085746493,-20.3689637094668,
5.75865365921882));
#145729=CARTESIAN_POINT('Ctrl Pts',(16.5560170315913,-20.2999111537828,
5.76276754104799));
#145730=CARTESIAN_POINT('Ctrl Pts',(16.5134482524877,-20.2285733472958,
5.76688142287716));
#145731=CARTESIAN_POINT('Ctrl Pts',(16.4744330306069,-20.1553108953332,
5.77099530470634));
#145732=CARTESIAN_POINT('Ctrl Pts',(16.4354291736147,-20.0820697842618,
5.77510798818763));
#145733=CARTESIAN_POINT('Ctrl Pts',(16.3999770407453,-20.0069055590536,
5.77922067166892));
#145734=CARTESIAN_POINT('Ctrl Pts',(16.3682620211175,-19.9302043831803,
5.78333335515021));
#145735=CARTESIAN_POINT('Ctrl Pts',(16.3361584999705,-19.852563635971,5.78749641803532));
#145736=CARTESIAN_POINT('Ctrl Pts',(16.3078844956127,-19.7733484709671,
5.79165948092042));
#145737=CARTESIAN_POINT('Ctrl Pts',(16.2835818660734,-19.6929797358388,
5.79582254380553));
#145738=CARTESIAN_POINT('Ctrl Pts',(16.2595524301165,-19.6135144512041,
5.79993880837768));
#145739=CARTESIAN_POINT('Ctrl Pts',(16.2394055983612,-19.5329218806178,
5.80405507294983));
#145740=CARTESIAN_POINT('Ctrl Pts',(16.2232275631065,-19.4516216269696,
5.80817133752197));
#145741=CARTESIAN_POINT('Ctrl Pts',(16.2067736327737,-19.3689349046017,
5.81235779956356));
#145742=CARTESIAN_POINT('Ctrl Pts',(16.1944252132089,-19.2855166404035,
5.81654426160515));
#145743=CARTESIAN_POINT('Ctrl Pts',(16.186218055036,-19.2018142528269,5.82073072364674));
#145744=CARTESIAN_POINT('Ctrl Pts',(16.1780108968631,-19.1181118652502,
5.82491718568833));
#145745=CARTESIAN_POINT('Ctrl Pts',(16.1739449655996,-19.0341258661345,
5.82910364772991));
#145746=CARTESIAN_POINT('Ctrl Pts',(16.1740005630998,-18.9503020392334,
5.8332901097715));
#145747=CARTESIAN_POINT('',(16.1740007055014,-18.9539005700932,5.76670989019962));
#145748=CARTESIAN_POINT('Ctrl Pts',(20.2935357468249,-20.9821350335323,
5.4833696516309));
#145749=CARTESIAN_POINT('Ctrl Pts',(20.2270815882697,-21.0331846603208,
5.48754740634818));
#145750=CARTESIAN_POINT('Ctrl Pts',(20.1580239132524,-21.0810403461138,
5.49172516106546));
#145751=CARTESIAN_POINT('Ctrl Pts',(20.0867037291457,-21.1254287706652,
5.49590291578274));
#145752=CARTESIAN_POINT('Ctrl Pts',(20.015460353698,-21.1697693908621,5.50007617124442));
#145753=CARTESIAN_POINT('Ctrl Pts',(19.9419597007997,-21.2106499296345,
5.5042494267061));
#145754=CARTESIAN_POINT('Ctrl Pts',(19.8665733495297,-21.2478391947031,
5.50842268216778));
#145755=CARTESIAN_POINT('Ctrl Pts',(19.7912312733654,-21.2850066181702,
5.51259348663769));
#145756=CARTESIAN_POINT('Ctrl Pts',(19.7140061091704,-21.3184868690186,
5.51676429110759));
#145757=CARTESIAN_POINT('Ctrl Pts',(19.635294757175,-21.3480942720788,5.5209350955775));
#145758=CARTESIAN_POINT('Ctrl Pts',(19.556606021274,-21.3776931680583,5.52510470165219));
#145759=CARTESIAN_POINT('Ctrl Pts',(19.4764323760497,-21.4034212646175,
5.52927430772688));
#145760=CARTESIAN_POINT('Ctrl Pts',(19.3951901898219,-21.4251412278484,
5.53344391380158));
#145761=CARTESIAN_POINT('Ctrl Pts',(19.3139469762852,-21.4468614657285,
5.53761357260102));
#145762=CARTESIAN_POINT('Ctrl Pts',(19.2316356396825,-21.4645733520643,
5.54178323140045));
#145763=CARTESIAN_POINT('Ctrl Pts',(19.1486858492173,-21.4781899466309,
5.54595289019989));
#145764=CARTESIAN_POINT('Ctrl Pts',(19.0656524537254,-21.4918202653521,
5.55012675159506));
#145765=CARTESIAN_POINT('Ctrl Pts',(18.9819797739384,-21.5013469721866,
5.55430061299022));
#145766=CARTESIAN_POINT('Ctrl Pts',(18.8981053133176,-21.5067347114996,
5.55847447438539));
#145767=CARTESIAN_POINT('Ctrl Pts',(18.8141902491749,-21.5121250590105,
5.56265035634165));
#145768=CARTESIAN_POINT('Ctrl Pts',(18.7300736701582,-21.5133724406709,
5.56682623829792));
#145769=CARTESIAN_POINT('Ctrl Pts',(18.6461933463466,-21.5104936958246,
5.57100212025418));
#145770=CARTESIAN_POINT('Ctrl Pts',(18.562161458039,-21.5076097493351,5.57518554766825));
#145771=CARTESIAN_POINT('Ctrl Pts',(18.4783671375726,-21.5005848165362,
5.57936897508233));
#145772=CARTESIAN_POINT('Ctrl Pts',(18.3952432446133,-21.4894877065081,
5.5835524024964));
#145773=CARTESIAN_POINT('Ctrl Pts',(18.3145513547331,-21.4787152709484,
5.58761343299197));
#145774=CARTESIAN_POINT('Ctrl Pts',(18.2344915683268,-21.4641058135859,
5.59167446348754));
#145775=CARTESIAN_POINT('Ctrl Pts',(18.1554472698611,-21.4457675790757,
5.59573549398311));
#145776=CARTESIAN_POINT('Ctrl Pts',(18.073997132933,-21.4268711913427,5.59992012837615));
#145777=CARTESIAN_POINT('Ctrl Pts',(17.9933221701874,-21.4039450190917,
5.60410476276919));
#145778=CARTESIAN_POINT('Ctrl Pts',(17.9138510440901,-21.3770681825714,
5.60828939716224));
#145779=CARTESIAN_POINT('Ctrl Pts',(17.8344930353044,-21.3502296019012,
5.61246807524617));
#145780=CARTESIAN_POINT('Ctrl Pts',(17.7563358916503,-21.3194516726889,
5.6166467533301));
#145781=CARTESIAN_POINT('Ctrl Pts',(17.6797967513082,-21.2848642288928,
5.62082543141404));
#145782=CARTESIAN_POINT('Ctrl Pts',(17.6018857018828,-21.2496568300241,
5.62507900929947));
#145783=CARTESIAN_POINT('Ctrl Pts',(17.5256517013921,-21.2105021111289,
5.62933258718491));
#145784=CARTESIAN_POINT('Ctrl Pts',(17.4515171985772,-21.1675897327923,
5.63358616507035));
#145785=CARTESIAN_POINT('Ctrl Pts',(17.378819937761,-21.1255092946465,5.6377572790483));
#145786=CARTESIAN_POINT('Ctrl Pts',(17.3081419118304,-21.0798158370634,
5.64192839302626));
#145787=CARTESIAN_POINT('Ctrl Pts',(17.2398584137968,-21.03073541375,5.64609950700422));
#145788=CARTESIAN_POINT('Ctrl Pts',(17.1715978289504,-20.9816714598466,
5.65026922132459));
#145789=CARTESIAN_POINT('Ctrl Pts',(17.105730549462,-20.929223065652,5.65443893564497));
#145790=CARTESIAN_POINT('Ctrl Pts',(17.0426026198917,-20.8736594137783,
5.65860864996535));
#145791=CARTESIAN_POINT('Ctrl Pts',(16.979476936684,-20.8180977390978,5.66277821590939));
#145792=CARTESIAN_POINT('Ctrl Pts',(16.9190907543433,-20.7594213317294,
5.66694778185343));
#145793=CARTESIAN_POINT('Ctrl Pts',(16.8617557221019,-20.6979385338201,
5.67111734779747));
#145794=CARTESIAN_POINT('Ctrl Pts',(16.8024048608573,-20.6342940765834,
5.67543351053639));
#145795=CARTESIAN_POINT('Ctrl Pts',(16.7463240583281,-20.5676425973542,
5.67974967327531));
#145796=CARTESIAN_POINT('Ctrl Pts',(16.6938147044707,-20.4983647564227,
5.68406583601423));
#145797=CARTESIAN_POINT('Ctrl Pts',(16.6430158372923,-20.4313436338728,
5.68824140020591));
#145798=CARTESIAN_POINT('Ctrl Pts',(16.595559538813,-20.36186504502,5.6924169643976));
#145799=CARTESIAN_POINT('Ctrl Pts',(16.5516743299492,-20.2903029066087,
5.69659252858928));
#145800=CARTESIAN_POINT('Ctrl Pts',(16.5055725835129,-20.215126334709,5.70097899060182));
#145801=CARTESIAN_POINT('Ctrl Pts',(16.4634124379743,-20.1376507144179,
5.70536545261436));
#145802=CARTESIAN_POINT('Ctrl Pts',(16.4254030213235,-20.0583362915703,
5.70975191462691));
#145803=CARTESIAN_POINT('Ctrl Pts',(16.3873936046727,-19.9790218687227,
5.71413837663945));
#145804=CARTESIAN_POINT('Ctrl Pts',(16.3535350701226,-19.897869208087,5.718524838652));
#145805=CARTESIAN_POINT('Ctrl Pts',(16.323976493569,-19.8153578044185,5.72291130066454));
#145806=CARTESIAN_POINT('Ctrl Pts',(16.2911969765866,-19.7238552940422,
5.72777574688618));
#145807=CARTESIAN_POINT('Ctrl Pts',(16.2636032939182,-19.630402505787,5.73264019310782));
#145808=CARTESIAN_POINT('Ctrl Pts',(16.2413973788046,-19.5355513454785,
5.73750463932946));
#145809=CARTESIAN_POINT('Ctrl Pts',(16.2191773325018,-19.4406398246901,
5.74237218114115));
#145810=CARTESIAN_POINT('Ctrl Pts',(16.2023520711407,-19.3443282665182,
5.74723972295285));
#145811=CARTESIAN_POINT('Ctrl Pts',(16.1910760934491,-19.2471914725933,
5.75210726476454));
#145812=CARTESIAN_POINT('Ctrl Pts',(16.1798001157575,-19.1500546786684,
5.75697480657623));
#145813=CARTESIAN_POINT('Ctrl Pts',(16.1740736044194,-19.0520927805192,
5.76184234838793));
#145814=CARTESIAN_POINT('Ctrl Pts',(16.1740007055014,-18.9539005700933,
5.76670989019962));
#145815=CARTESIAN_POINT('Ctrl Pts',(16.174000705501,-18.9539005695105,5.76670989022851));
#145816=CARTESIAN_POINT('Ctrl Pts',(16.1739381768052,-18.8696766480678,
5.77088500205647));
#145817=CARTESIAN_POINT('Ctrl Pts',(16.1780364138872,-18.7854119279347,
5.77506011388444));
#145818=CARTESIAN_POINT('Ctrl Pts',(16.1862808495761,-18.7015461508315,
5.7792352257124));
#145819=CARTESIAN_POINT('Ctrl Pts',(16.1945245019764,-18.617688341661,5.78340994087069));
#145820=CARTESIAN_POINT('Ctrl Pts',(16.2069135252697,-18.5342298557721,
5.78758465602899));
#145821=CARTESIAN_POINT('Ctrl Pts',(16.2233814427541,-18.4516056954636,
5.79175937118728));
#145822=CARTESIAN_POINT('Ctrl Pts',(16.2398526754154,-18.3689649019825,
5.79593492676267));
#145823=CARTESIAN_POINT('Ctrl Pts',(16.2604043427349,-18.2871592164315,
5.80011048233807));
#145824=CARTESIAN_POINT('Ctrl Pts',(16.2849190524512,-18.2066125085881,
5.80428603791346));
#145825=CARTESIAN_POINT('Ctrl Pts',(16.3094630809747,-18.1259694694634,
5.80846658731951));
#145826=CARTESIAN_POINT('Ctrl Pts',(16.3379794801119,-18.0465888526479,
5.81264713672555));
#145827=CARTESIAN_POINT('Ctrl Pts',(16.370301376024,-17.9688780263803,5.8168276861316));
#145828=CARTESIAN_POINT('Ctrl Pts',(16.4026440716432,-17.8911171918327,
5.82101092579452));
#145829=CARTESIAN_POINT('Ctrl Pts',(16.4387969424267,-17.815028700182,5.82519416545745));
#145830=CARTESIAN_POINT('Ctrl Pts',(16.4785465454209,-17.7409964020585,
5.82937740512037));
#145831=CARTESIAN_POINT('Ctrl Pts',(16.5183679957913,-17.6668302906143,
5.8335682059857));
#145832=CARTESIAN_POINT('Ctrl Pts',(16.5617989238527,-17.5947281861652,
5.83775900685103));
#145833=CARTESIAN_POINT('Ctrl Pts',(16.6085819963934,-17.5250457926251,
5.84194980771636));
#145834=CARTESIAN_POINT('Ctrl Pts',(16.6388616407137,-17.4799449051204,
5.84466224092623));
#145835=CARTESIAN_POINT('Ctrl Pts',(16.67054468148,-17.4358570345709,5.8473746741361));
#145836=CARTESIAN_POINT('Ctrl Pts',(16.7035527014987,-17.392870830236,5.85008710734598));
#145837=CARTESIAN_POINT('Ctrl Pts',(16.754476165831,-17.3265534188316,5.85427174173903));
#145838=CARTESIAN_POINT('Ctrl Pts',(16.8087468503132,-17.262610070515,5.85845637613208));
#145839=CARTESIAN_POINT('Ctrl Pts',(16.8661152556942,-17.2013982228989,
5.86264101052513));
#145840=CARTESIAN_POINT('Ctrl Pts',(16.9234020042509,-17.1402735027714,
5.86681968860908));
#145841=CARTESIAN_POINT('Ctrl Pts',(16.9837774037106,-17.0818728934346,
5.87099836669302));
#145842=CARTESIAN_POINT('Ctrl Pts',(17.0469505633859,-17.0265223453854,
5.87517704477697));
#145843=CARTESIAN_POINT('Ctrl Pts',(17.1112560565466,-16.9701796785422,
5.87943062266241));
#145844=CARTESIAN_POINT('Ctrl Pts',(17.1784603025304,-16.9169978755986,
5.88368420054784));
#145845=CARTESIAN_POINT('Ctrl Pts',(17.2482157539324,-16.8672829510609,
5.88793777843328));
#145846=CARTESIAN_POINT('Ctrl Pts',(17.3166188597925,-16.818531847346,5.89210889241123));
#145847=CARTESIAN_POINT('Ctrl Pts',(17.3874747417498,-16.773114676503,5.89628000638918));
#145848=CARTESIAN_POINT('Ctrl Pts',(17.4604222489457,-16.7312794610714,
5.90045112036713));
#145849=CARTESIAN_POINT('Ctrl Pts',(17.5333452779011,-16.6894582838502,
5.9046208346875));
#145850=CARTESIAN_POINT('Ctrl Pts',(17.6083581394479,-16.6512169036012,
5.90879054900788));
#145851=CARTESIAN_POINT('Ctrl Pts',(17.6850725337916,-16.6167588624226,
5.91296026332825));
#145852=CARTESIAN_POINT('Ctrl Pts',(17.7617841983079,-16.582302047409,5.9171298292723));
#145853=CARTESIAN_POINT('Ctrl Pts',(17.8401968552436,-16.5516284915071,
5.92129939521634));
#145854=CARTESIAN_POINT('Ctrl Pts',(17.9199008000001,-16.5248942147983,
5.92546896116039));
#145855=CARTESIAN_POINT('Ctrl Pts',(18.0024070371288,-16.4972199939007,
5.92978512389931));
#145856=CARTESIAN_POINT('Ctrl Pts',(18.0862965548759,-16.4737673840696,
5.93410128663823));
#145857=CARTESIAN_POINT('Ctrl Pts',(18.1710980677306,-16.4546531248848,
5.93841744937714));
#145858=CARTESIAN_POINT('Ctrl Pts',(18.2531371802236,-16.4361615106825,
5.94259301356882));
#145859=CARTESIAN_POINT('Ctrl Pts',(18.3360293116304,-16.4217299783601,
5.9467685777605));
#145860=CARTESIAN_POINT('Ctrl Pts',(18.4193394847883,-16.411411729507,5.95094414195217));
#145861=CARTESIAN_POINT('Ctrl Pts',(18.5068574567414,-16.4005723304336,
5.95533060396471));
#145862=CARTESIAN_POINT('Ctrl Pts',(18.5948362284719,-16.3942727005953,
5.95971706597725));
#145863=CARTESIAN_POINT('Ctrl Pts',(18.682770269855,-16.3925126461048,5.96410352798979));
#145864=CARTESIAN_POINT('Ctrl Pts',(18.7707043112381,-16.3907525916143,
5.96848999000233));
#145865=CARTESIAN_POINT('Ctrl Pts',(18.8585930447509,-16.3935320181048,
5.97287645201487));
#145866=CARTESIAN_POINT('Ctrl Pts',(18.9459382820312,-16.4007880988421,
5.97726291402741));
#145867=CARTESIAN_POINT('Ctrl Pts',(19.0292646354676,-16.4077103165486,
5.98144754842046));
#145868=CARTESIAN_POINT('Ctrl Pts',(19.1124065643328,-16.4187320520138,
5.9856321828135));
#145869=CARTESIAN_POINT('Ctrl Pts',(19.1949284709478,-16.4338369900521,
5.98981681720655));
#145870=CARTESIAN_POINT('Ctrl Pts',(19.2773329178427,-16.4489204280808,
5.99399549529048));
#145871=CARTESIAN_POINT('Ctrl Pts',(19.3591186468153,-16.4680754422333,
5.99817417337441));
#145872=CARTESIAN_POINT('Ctrl Pts',(19.4398541314688,-16.491233870298,6.00235285145835));
#145873=CARTESIAN_POINT('Ctrl Pts',(19.5220367416614,-16.5148073965422,
6.00660642934378));
#145874=CARTESIAN_POINT('Ctrl Pts',(19.6031306054559,-16.5425292308513,
6.01086000722922));
#145875=CARTESIAN_POINT('Ctrl Pts',(19.682690292262,-16.5742727807068,6.01511358511466));
#145876=CARTESIAN_POINT('Ctrl Pts',(19.7607075592913,-16.6054009199058,
6.01928469909261));
#145877=CARTESIAN_POINT('Ctrl Pts',(19.8372491575625,-16.6403960502729,
6.02345581307056));
#145878=CARTESIAN_POINT('Ctrl Pts',(19.9119110552604,-16.6790887509858,
6.02762692704851));
#145879=CARTESIAN_POINT('Ctrl Pts',(19.9865478994375,-16.7177684679893,
6.03179664136888));
#145880=CARTESIAN_POINT('Ctrl Pts',(20.059305887621,-16.7601430796837,6.03596635568925));
#145881=CARTESIAN_POINT('Ctrl Pts',(20.1298036938035,-16.805996260869,6.04013607000962));
#145882=CARTESIAN_POINT('Ctrl Pts',(20.2002989913718,-16.8518478104014,
6.04430563595367));
#145883=CARTESIAN_POINT('Ctrl Pts',(20.2685338816756,-16.9011774317726,
6.04847520189772));
#145884=CARTESIAN_POINT('Ctrl Pts',(20.3341554111886,-16.9537250789634,
6.05264476784177));
#145885=CARTESIAN_POINT('Ctrl Pts',(20.4020841127263,-17.0081202366048,
6.0569609305807));
#145886=CARTESIAN_POINT('Ctrl Pts',(20.4672118510044,-17.0659635923385,
6.06127709331962));
#145887=CARTESIAN_POINT('Ctrl Pts',(20.5291853686021,-17.1269220585529,
6.06559325605854));
#145888=CARTESIAN_POINT('Ctrl Pts',(20.5891401053826,-17.185894809142,6.06976882025022));
#145889=CARTESIAN_POINT('Ctrl Pts',(20.6461426787832,-17.2477824589604,
6.07394438444191));
#145890=CARTESIAN_POINT('Ctrl Pts',(20.6999129097985,-17.3122480580625,
6.07811994863359));
#145891=CARTESIAN_POINT('Ctrl Pts',(20.7563989473557,-17.3799696613228,
6.08250641064613));
#145892=CARTESIAN_POINT('Ctrl Pts',(20.8093171796,-17.4505360152562,6.08689287265867));
#145893=CARTESIAN_POINT('Ctrl Pts',(20.8583941356916,-17.523521944082,6.09127933467122));
#145894=CARTESIAN_POINT('Ctrl Pts',(20.9074710917831,-17.5965078729078,
6.09566579668376));
#145895=CARTESIAN_POINT('Ctrl Pts',(20.9527065384673,-17.6719128399418,
6.1000522586963));
#145896=CARTESIAN_POINT('Ctrl Pts',(20.9938836431733,-17.7492839406918,
6.10443872070884));
#145897=CARTESIAN_POINT('Ctrl Pts',(21.0331661282526,-17.8230950824048,
6.10862335510189));
#145898=CARTESIAN_POINT('Ctrl Pts',(21.0689017421373,-17.8989701434485,
6.11280798949494));
#145899=CARTESIAN_POINT('Ctrl Pts',(21.1008684225542,-17.9765340240092,
6.11699262388799));
#145900=CARTESIAN_POINT('Ctrl Pts',(21.1327896023583,-18.0539875019864,
6.12117130197193));
#145901=CARTESIAN_POINT('Ctrl Pts',(21.1609523307066,-18.1331246030375,
6.12534998005586));
#145902=CARTESIAN_POINT('Ctrl Pts',(21.1851803441782,-18.2135455868408,
6.1295286581398));
#145903=CARTESIAN_POINT('Ctrl Pts',(21.209842627379,-18.2954080589815,6.13378223602524));
#145904=CARTESIAN_POINT('Ctrl Pts',(21.2304275222057,-18.3786004681758,
6.13803581391068));
#145905=CARTESIAN_POINT('Ctrl Pts',(21.2468003698022,-18.462679755659,6.14228939179611));
#145906=CARTESIAN_POINT('Ctrl Pts',(21.2628557977991,-18.5451290020871,
6.14646050577407));
#145907=CARTESIAN_POINT('Ctrl Pts',(21.2748609466778,-18.6284305735953,
6.15063161975202));
#145908=CARTESIAN_POINT('Ctrl Pts',(21.2827395777799,-18.7121530390886,
6.15480273372997));
#145909=CARTESIAN_POINT('Ctrl Pts',(21.2906155651312,-18.7958474107,6.15897244805034));
#145910=CARTESIAN_POINT('Ctrl Pts',(21.2943677416632,-18.8799619381733,
6.16314216237071));
#145911=CARTESIAN_POINT('Ctrl Pts',(21.2939715980996,-18.9640588939544,
6.16731187669109));
#145912=CARTESIAN_POINT('Ctrl Pts',(21.2935754686325,-19.0481528572048,
6.17148144263512));
#145913=CARTESIAN_POINT('Ctrl Pts',(21.2890313155855,-19.1322287899825,
6.17565100857916));
#145914=CARTESIAN_POINT('Ctrl Pts',(21.2803667494582,-19.2158491562499,
6.1798205745232));
#145915=CARTESIAN_POINT('Ctrl Pts',(21.2713975478748,-19.3024095114386,
6.18413673726212));
#145916=CARTESIAN_POINT('Ctrl Pts',(21.2580128490968,-19.3884811440151,
6.18845290000104));
#145917=CARTESIAN_POINT('Ctrl Pts',(21.2403015155519,-19.4735867263861,
6.19276906273997));
#145918=CARTESIAN_POINT('Ctrl Pts',(21.2231671268343,-19.5559200033628,
6.19694462693165));
#145919=CARTESIAN_POINT('Ctrl Pts',(21.2019838191124,-19.6373487577945,
6.20112019112333));
#145920=CARTESIAN_POINT('Ctrl Pts',(21.1768832583853,-19.7174550188619,
6.20529575531501));
#145921=CARTESIAN_POINT('Ctrl Pts',(21.1505149280068,-19.8016072567413,
6.20968221732755));
#145922=CARTESIAN_POINT('Ctrl Pts',(21.1198234271566,-19.8842993445544,
6.2140686793401));
#145923=CARTESIAN_POINT('Ctrl Pts',(21.085018236802,-19.9650711970166,6.21845514135264));
#145924=CARTESIAN_POINT('Ctrl Pts',(21.0502130464473,-20.0458430494787,
6.22284160336519));
#145925=CARTESIAN_POINT('Ctrl Pts',(21.0112944915985,-20.1246941799627,
6.22722806537773));
#145926=CARTESIAN_POINT('Ctrl Pts',(20.9685260259017,-20.2011971179794,
6.23161452739028));
#145927=CARTESIAN_POINT('Ctrl Pts',(20.926496351346,-20.2763785287457,6.23592521676934));
#145928=CARTESIAN_POINT('Ctrl Pts',(20.8805876001805,-20.3495805638946,
6.24023590614841));
#145929=CARTESIAN_POINT('Ctrl Pts',(20.8310139355987,-20.420377524312,6.24454659552748));
#145930=CARTESIAN_POINT('Ctrl Pts',(20.7829663020667,-20.4889951348523,
6.24872458852646));
#145931=CARTESIAN_POINT('Ctrl Pts',(20.7314763645207,-20.555353152089,6.25290258152543));
#145932=CARTESIAN_POINT('Ctrl Pts',(20.6767860610052,-20.6190879764319,
6.25708057452441));
#145933=CARTESIAN_POINT('Ctrl Pts',(20.6194902461936,-20.6858592038318,
6.26145761209352));
#145934=CARTESIAN_POINT('Ctrl Pts',(20.5586817759822,-20.7497506182763,
6.26583464966264));
#145935=CARTESIAN_POINT('Ctrl Pts',(20.4946892619671,-20.8103792193182,
6.27021168723176));
#145936=CARTESIAN_POINT('Ctrl Pts',(20.430696747952,-20.8710078203602,6.27458872480087));
#145937=CARTESIAN_POINT('Ctrl Pts',(20.363520576587,-20.9283731694461,6.27896576236998));
#145938=CARTESIAN_POINT('Ctrl Pts',(20.2935357468249,-20.9821350335323,
6.2833427999391));
#145939=CARTESIAN_POINT('Origin',(18.734,-18.952,-1.76670989022851));
#145940=CARTESIAN_POINT('',(20.2935357468249,-20.9821350335323,7.14996297925329));
#145941=CARTESIAN_POINT('',(20.2935357468249,-20.9821350335323,7.08324142646255));
#145942=CARTESIAN_POINT('',(20.2935357468249,-20.9821350335323,-1.76670989022851));
#145943=CARTESIAN_POINT('',(16.1740008768645,-18.954118854712,6.6332901097715));
#145944=CARTESIAN_POINT('Ctrl Pts',(16.1740008768645,-18.954118854712,6.6332901097715));
#145945=CARTESIAN_POINT('Ctrl Pts',(16.1739325519701,-18.8715687540989,
6.63740642252224));
#145946=CARTESIAN_POINT('Ctrl Pts',(16.1778613169669,-18.7888758591841,
6.64152273527298));
#145947=CARTESIAN_POINT('Ctrl Pts',(16.1858020059738,-18.7064659224448,
6.64563904802372));
#145948=CARTESIAN_POINT('Ctrl Pts',(16.1937337220434,-18.624149108506,6.64975070936243));
#145949=CARTESIAN_POINT('Ctrl Pts',(16.2056683130375,-18.5421150878493,
6.65386237070115));
#145950=CARTESIAN_POINT('Ctrl Pts',(16.2215685692311,-18.4607889397778,
6.65797403203986));
#145951=CARTESIAN_POINT('Ctrl Pts',(16.2374592000152,-18.3795120234588,
6.6620832043354));
#145952=CARTESIAN_POINT('Ctrl Pts',(16.2573106430753,-18.2989425946372,
6.66619237663094));
#145953=CARTESIAN_POINT('Ctrl Pts',(16.2810340922893,-18.219498630985,6.67030154892649));
#145954=CARTESIAN_POINT('Ctrl Pts',(16.3047507902538,-18.1400772755974,
6.67440955182854));
#145955=CARTESIAN_POINT('Ctrl Pts',(16.3323371713263,-18.0617812045222,
6.67851755473059));
#145956=CARTESIAN_POINT('Ctrl Pts',(16.3636541468014,-17.9850147176797,
6.68262555763264));
#145957=CARTESIAN_POINT('Ctrl Pts',(16.3949722554067,-17.9082454532245,
6.686733709173));
#145958=CARTESIAN_POINT('Ctrl Pts',(16.4300210447237,-17.8330063217983,
6.69084186071336));
#145959=CARTESIAN_POINT('Ctrl Pts',(16.4686133150906,-17.7596815996408,
6.69495001225373));
#145960=CARTESIAN_POINT('Ctrl Pts',(16.5072438266208,-17.6862842198592,
6.69906223457025));
#145961=CARTESIAN_POINT('Ctrl Pts',(16.5494246053548,-17.6148054564872,
6.70317445688677));
#145962=CARTESIAN_POINT('Ctrl Pts',(16.5949228757402,-17.5456042319217,
6.70728667920329));
#145963=CARTESIAN_POINT('Ctrl Pts',(16.6404458510681,-17.4763654320318,
6.71140113440064));
#145964=CARTESIAN_POINT('Ctrl Pts',(16.6892896206455,-17.4094070139063,
6.71551558959799));
#145965=CARTESIAN_POINT('Ctrl Pts',(16.7411800554791,-17.3450561090319,
6.71963004479534));
#145966=CARTESIAN_POINT('Ctrl Pts',(16.7931561866084,-17.2805989295773,
6.72375129495539));
#145967=CARTESIAN_POINT('Ctrl Pts',(16.8481887081044,-17.2187582108671,
6.72787254511545));
#145968=CARTESIAN_POINT('Ctrl Pts',(16.9059658904507,-17.1598249822285,
6.73199379527551));
#145969=CARTESIAN_POINT('Ctrl Pts',(16.9382542996129,-17.1268905239829,
6.73429692959297));
#145970=CARTESIAN_POINT('Ctrl Pts',(16.9713992632832,-17.0948633881751,
6.73660006391043));
#145971=CARTESIAN_POINT('Ctrl Pts',(17.0053421035808,-17.0637887096123,
6.73890319822789));
#145972=CARTESIAN_POINT('Ctrl Pts',(17.067013876621,-17.0073281863675,6.74308783262094));
#145973=CARTESIAN_POINT('Ctrl Pts',(17.1315694533285,-16.9537872066973,
6.74727246701399));
#145974=CARTESIAN_POINT('Ctrl Pts',(17.1987010234279,-16.9034744198481,
6.75145710140704));
#145975=CARTESIAN_POINT('Ctrl Pts',(17.2657370400464,-16.8532332470236,
6.75563577949098));
#145976=CARTESIAN_POINT('Ctrl Pts',(17.3353414020478,-16.8062114135714,
6.75981445757493));
#145977=CARTESIAN_POINT('Ctrl Pts',(17.4071710083241,-16.7626793686515,
6.76399313565888));
#145978=CARTESIAN_POINT('Ctrl Pts',(17.4802881086697,-16.7183670431123,
6.76824671354431));
#145979=CARTESIAN_POINT('Ctrl Pts',(17.5557106573433,-16.6776711711576,
6.77250029142975));
#145980=CARTESIAN_POINT('Ctrl Pts',(17.6330432222703,-16.6408327248832,
6.77675386931518));
#145981=CARTESIAN_POINT('Ctrl Pts',(17.7088765445241,-16.6047084637741,
6.78092498329313));
#145982=CARTESIAN_POINT('Ctrl Pts',(17.7865460506903,-16.5722936025649,
6.78509609727108));
#145983=CARTESIAN_POINT('Ctrl Pts',(17.8656529884826,-16.5437696398416,
6.78926721124903));
#145984=CARTESIAN_POINT('Ctrl Pts',(17.9447333811778,-16.5152552486095,
6.7934369255694));
#145985=CARTESIAN_POINT('Ctrl Pts',(18.0252498151565,-16.4906293187767,
6.79760663988977));
#145986=CARTESIAN_POINT('Ctrl Pts',(18.1067845307984,-16.4700248278449,
6.80177635421014));
#145987=CARTESIAN_POINT('Ctrl Pts',(18.1883163450853,-16.4494210701093,
6.80594592015419));
#145988=CARTESIAN_POINT('Ctrl Pts',(18.2708659227707,-16.4328385786397,
6.81011548609823));
#145989=CARTESIAN_POINT('Ctrl Pts',(18.3540026821446,-16.4203598126071,
6.81428505204228));
#145990=CARTESIAN_POINT('Ctrl Pts',(18.4400624274178,-16.407442308555,6.8186012147812));
#145991=CARTESIAN_POINT('Ctrl Pts',(18.5267508916658,-16.3989225513938,
6.82291737752012));
#145992=CARTESIAN_POINT('Ctrl Pts',(18.6135836740995,-16.3948336173693,
6.82723354025904));
#145993=CARTESIAN_POINT('Ctrl Pts',(18.6975878877786,-16.3908778799405,
6.83140910445072));
#145994=CARTESIAN_POINT('Ctrl Pts',(18.7817266907699,-16.3910686822566,
6.8355846686424));
#145995=CARTESIAN_POINT('Ctrl Pts',(18.8655624783154,-16.3953828377523,
6.83976023283408));
#145996=CARTESIAN_POINT('Ctrl Pts',(18.9536326121891,-16.3999148909862,
6.84414669484662));
#145997=CARTESIAN_POINT('Ctrl Pts',(19.0413677347563,-16.4089977253143,
6.84853315685916));
#145998=CARTESIAN_POINT('Ctrl Pts',(19.1282700391326,-16.4225433120446,
6.8529196188717));
#145999=CARTESIAN_POINT('Ctrl Pts',(19.2151723435089,-16.4360888987749,
6.85730608088424));
#146000=CARTESIAN_POINT('Ctrl Pts',(19.3012412773527,-16.4540970446291,
6.86169254289678));
#146001=CARTESIAN_POINT('Ctrl Pts',(19.3859971465594,-16.4764193164273,
6.86607900490932));
#146002=CARTESIAN_POINT('Ctrl Pts',(19.4668532725857,-16.4977145074105,
6.87026363930238));
#146003=CARTESIAN_POINT('Ctrl Pts',(19.5468154727232,-16.5230148144696,
6.87444827369543));
#146004=CARTESIAN_POINT('Ctrl Pts',(19.6254576099361,-16.5522284838579,
6.87863290808848));
#146005=CARTESIAN_POINT('Ctrl Pts',(19.7039878098006,-16.5814005712038,
6.88281158617243));
#146006=CARTESIAN_POINT('Ctrl Pts',(19.7812012513676,-16.6144747979098,
6.88699026425638));
#146007=CARTESIAN_POINT('Ctrl Pts',(19.8566848155709,-16.6513090592419,
6.89116894234032));
#146008=CARTESIAN_POINT('Ctrl Pts',(19.9335213684134,-16.688803548236,6.89542252022576));
#146009=CARTESIAN_POINT('Ctrl Pts',(20.0085649515612,-16.7301940721625,
6.89967609811119));
#146010=CARTESIAN_POINT('Ctrl Pts',(20.0813989057343,-16.7752785688504,
6.90392967599663));
#146011=CARTESIAN_POINT('Ctrl Pts',(20.1528208315821,-16.8194890145949,
6.90810078997458));
#146012=CARTESIAN_POINT('Ctrl Pts',(20.2221176306652,-16.8672512282388,
6.91227190395253));
#146013=CARTESIAN_POINT('Ctrl Pts',(20.2889208543458,-16.9183281639555,
6.91644301793049));
#146014=CARTESIAN_POINT('Ctrl Pts',(20.3557016615595,-16.9693879603131,
6.92061273225086));
#146015=CARTESIAN_POINT('Ctrl Pts',(20.4199901900087,-17.0237599905365,
6.92478244657124));
#146016=CARTESIAN_POINT('Ctrl Pts',(20.4814485012998,-17.0811649630966,
6.92895216089161));
#146017=CARTESIAN_POINT('Ctrl Pts',(20.5429046256404,-17.1385678929415,
6.93312172683566));
#146018=CARTESIAN_POINT('Ctrl Pts',(20.6015303974547,-17.1990032359004,
6.9372912927797));
#146019=CARTESIAN_POINT('Ctrl Pts',(20.6570234159163,-17.2621535744815,
6.94146085872375));
#146020=CARTESIAN_POINT('Ctrl Pts',(20.7144675004489,-17.3275242010627,
6.94577702146266));
#146021=CARTESIAN_POINT('Ctrl Pts',(20.7685540894613,-17.395803897787,6.95009318420158));
#146022=CARTESIAN_POINT('Ctrl Pts',(20.8189931741054,-17.4666032637932,
6.9544093469405));
#146023=CARTESIAN_POINT('Ctrl Pts',(20.8677892108726,-17.5350963478986,
6.95858491113218));
#146024=CARTESIAN_POINT('Ctrl Pts',(20.9131715145605,-17.6059470436349,
6.96276047532386));
#146025=CARTESIAN_POINT('Ctrl Pts',(20.9549227142454,-17.6787748442051,
6.96693603951554));
#146026=CARTESIAN_POINT('Ctrl Pts',(20.9987826677722,-17.7552810038503,
6.97132250152808));
#146027=CARTESIAN_POINT('Ctrl Pts',(21.0386347993093,-17.8339687234974,
6.97570896354062));
#146028=CARTESIAN_POINT('Ctrl Pts',(21.074283673631,-17.9143717780746,6.98009542555315));
#146029=CARTESIAN_POINT('Ctrl Pts',(21.1099325479527,-17.9947748326519,
6.98448188756569));
#146030=CARTESIAN_POINT('Ctrl Pts',(21.1413780286033,-18.0768926531098,
6.98886834957823));
#146031=CARTESIAN_POINT('Ctrl Pts',(21.1684852750765,-18.1602415485544,
6.99325481159076));
#146032=CARTESIAN_POINT('Ctrl Pts',(21.194345276957,-18.2397554377671,6.99743944598381));
#146033=CARTESIAN_POINT('Ctrl Pts',(21.216353744912,-18.320685570143,7.00162408037686));
#146034=CARTESIAN_POINT('Ctrl Pts',(21.2343571694271,-18.4026239673098,
7.00580871476991));
#146035=CARTESIAN_POINT('Ctrl Pts',(21.2523349682957,-18.48444573531,7.00998739285385));
#146036=CARTESIAN_POINT('Ctrl Pts',(21.2663189491972,-18.5672724719892,
7.01416607093779));
#146037=CARTESIAN_POINT('Ctrl Pts',(21.2762049862094,-18.650679890993,7.01834474902173));
#146038=CARTESIAN_POINT('Ctrl Pts',(21.2862682233301,-18.7355823280387,
7.02259832690716));
#146039=CARTESIAN_POINT('Ctrl Pts',(21.2920850111441,-18.8210860111296,
7.0268519047926));
#146040=CARTESIAN_POINT('Ctrl Pts',(21.2935997221946,-18.9067312233282,
7.03110548267803));
#146041=CARTESIAN_POINT('Ctrl Pts',(21.2950850676157,-18.9907160359654,
7.03527659665599));
#146042=CARTESIAN_POINT('Ctrl Pts',(21.2924336475012,-19.0748364579016,
7.03944771063394));
#146043=CARTESIAN_POINT('Ctrl Pts',(21.2856453456188,-19.1586543737303,
7.0436188246119));
#146044=CARTESIAN_POINT('Ctrl Pts',(21.2788593216166,-19.2424441636478,
7.04778853893227));
#146045=CARTESIAN_POINT('Ctrl Pts',(21.2679392098803,-19.3259311909062,
7.05195825325264));
#146046=CARTESIAN_POINT('Ctrl Pts',(21.2529369307439,-19.4086801275887,
7.05612796757301));
#146047=CARTESIAN_POINT('Ctrl Pts',(21.237935185453,-19.491426119709,7.06029753351705));
#146048=CARTESIAN_POINT('Ctrl Pts',(21.2188516444823,-19.573433620972,7.0644670994611));
#146049=CARTESIAN_POINT('Ctrl Pts',(21.1957895218783,-19.6542765480707,
7.06863666540515));
#146050=CARTESIAN_POINT('Ctrl Pts',(21.1719165634938,-19.7379618127557,
7.07295282814407));
#146051=CARTESIAN_POINT('Ctrl Pts',(21.143780188844,-19.8203985795368,7.07726899088298));
#146052=CARTESIAN_POINT('Ctrl Pts',(21.1115508461403,-19.9011322215674,
7.0815851536219));
#146053=CARTESIAN_POINT('Ctrl Pts',(21.0803713708853,-19.9792359737004,
7.08576071781358));
#146054=CARTESIAN_POINT('Ctrl Pts',(21.0453617283796,-20.0557454470089,
7.08993628200526));
#146055=CARTESIAN_POINT('Ctrl Pts',(21.0067242058648,-20.1302719058334,
7.09411184619694));
#146056=CARTESIAN_POINT('Ctrl Pts',(20.9661351939396,-20.2085625189234,
7.09849830820948));
#146057=CARTESIAN_POINT('Ctrl Pts',(20.9215424772636,-20.284664025024,7.10288477022202));
#146058=CARTESIAN_POINT('Ctrl Pts',(20.8732322919593,-20.3581597352501,
7.10727123223456));
#146059=CARTESIAN_POINT('Ctrl Pts',(20.824922106655,-20.4316554454762,7.11165769424711));
#146060=CARTESIAN_POINT('Ctrl Pts',(20.7728948573421,-20.5025449370744,
7.11604415625965));
#146061=CARTESIAN_POINT('Ctrl Pts',(20.7174842649082,-20.5704530178111,
7.12043061827219));
#146062=CARTESIAN_POINT('Ctrl Pts',(20.6646206180301,-20.6352397064664,
7.1246154567424));
#146063=CARTESIAN_POINT('Ctrl Pts',(20.6084810526635,-20.6975542088253,
7.12880029521261));
#146064=CARTESIAN_POINT('Ctrl Pts',(20.5493255613569,-20.7570465662371,
7.13298513368282));
#146065=CARTESIAN_POINT('Ctrl Pts',(20.4902614757663,-20.816446997415,7.13716350583606));
#146066=CARTESIAN_POINT('Ctrl Pts',(20.4281910470698,-20.8730336263624,
7.14134187798931));
#146067=CARTESIAN_POINT('Ctrl Pts',(20.3634146060857,-20.9264893115626,
7.14552025014255));
#146068=CARTESIAN_POINT('Ctrl Pts',(20.3404563686433,-20.9454352168149,
7.14700115984613));
#146069=CARTESIAN_POINT('Ctrl Pts',(20.3171585752192,-20.9639881395014,
7.14848206954971));
#146070=CARTESIAN_POINT('Ctrl Pts',(20.2935357468249,-20.9821350335323,
7.14996297925329));
#146071=CARTESIAN_POINT('Ctrl Pts',(20.2958869033725,-20.9851650055234,
6.34984102531927));
#146072=CARTESIAN_POINT('Ctrl Pts',(20.256159849257,-21.0159980900227,6.35235260960738));
#146073=CARTESIAN_POINT('Ctrl Pts',(19.5288319784645,-21.5446793381704,
6.39725612945596));
#146074=CARTESIAN_POINT('Ctrl Pts',(17.5479307767974,-21.7370548235123,
6.48455158486502));
#146075=CARTESIAN_POINT('Ctrl Pts',(16.247850859816,-20.0919179750469,6.57652302872766));
#146076=CARTESIAN_POINT('Ctrl Pts',(16.1710772471096,-19.0983559299756,
6.62610253702982));
#146077=CARTESIAN_POINT('Ctrl Pts',(16.1723626618067,-18.9541202106264,
6.6332901097715));
#146078=CARTESIAN_POINT('',(16.174000571626,-18.9502892327451,6.56670989025839));
#146079=CARTESIAN_POINT('Ctrl Pts',(20.2935357468249,-20.9821350335323,
6.2833427999391));
#146080=CARTESIAN_POINT('Ctrl Pts',(20.2268670566194,-21.0333494620566,
6.28751243731202));
#146081=CARTESIAN_POINT('Ctrl Pts',(20.1576502309574,-21.081293830517,6.29168207468495));
#146082=CARTESIAN_POINT('Ctrl Pts',(20.0862433854993,-21.1257152128035,
6.29585171205787));
#146083=CARTESIAN_POINT('Ctrl Pts',(20.0148367451412,-21.1701364674997,
6.30002133745445));
#146084=CARTESIAN_POINT('Ctrl Pts',(19.9412404887745,-21.2110345141912,
6.30419096285104));
#146085=CARTESIAN_POINT('Ctrl Pts',(19.8658401818764,-21.2482007322292,
6.30836058824763));
#146086=CARTESIAN_POINT('Ctrl Pts',(19.7898457788971,-21.2856597913099,
6.3125630670663));
#146087=CARTESIAN_POINT('Ctrl Pts',(19.7120191890284,-21.3193277301869,
6.31676554588497));
#146088=CARTESIAN_POINT('Ctrl Pts',(19.6327770921237,-21.3490397866272,
6.32096802470365));
#146089=CARTESIAN_POINT('Ctrl Pts',(19.5540386680255,-21.3785629894727,
6.32514379203458));
#146090=CARTESIAN_POINT('Ctrl Pts',(19.4739031398565,-21.4041803691427,
6.32931955936551));
#146091=CARTESIAN_POINT('Ctrl Pts',(19.3927942500441,-21.4257805351544,
6.33349532669644));
#146092=CARTESIAN_POINT('Ctrl Pts',(19.3109071059811,-21.447587958608,6.33771116125899));
#146093=CARTESIAN_POINT('Ctrl Pts',(19.2280282903973,-21.4653005647945,
6.34192699582153));
#146094=CARTESIAN_POINT('Ctrl Pts',(19.1446022367281,-21.4788569020018,
6.34614283038408));
#146095=CARTESIAN_POINT('Ctrl Pts',(19.0611761830589,-21.492413239209,6.35035866494663));
#146096=CARTESIAN_POINT('Ctrl Pts',(18.9772033709819,-21.5018133183543,
6.35457449950917));
#146097=CARTESIAN_POINT('Ctrl Pts',(18.8931294701917,-21.5070494734381,
6.35879033407172));
#146098=CARTESIAN_POINT('Ctrl Pts',(18.8096777759696,-21.512246877256,6.36297496846477));
#146099=CARTESIAN_POINT('Ctrl Pts',(18.7258158815286,-21.5133611702432,
6.36715960285782));
#146100=CARTESIAN_POINT('Ctrl Pts',(18.6419771668657,-21.5103455197025,
6.37134423725086));
#146101=CARTESIAN_POINT('Ctrl Pts',(18.5582577862359,-21.5073341615672,
6.3755229153348));
#146102=CARTESIAN_POINT('Ctrl Pts',(18.4745619756521,-21.5002045527773,
6.37970159341874));
#146103=CARTESIAN_POINT('Ctrl Pts',(18.3913265823787,-21.4889617515555,
6.38388027150268));
#146104=CARTESIAN_POINT('Ctrl Pts',(18.306599254501,-21.4775174312019,6.38813384938812));
#146105=CARTESIAN_POINT('Ctrl Pts',(18.2223494934531,-21.4618109801083,
6.39238742727355));
#146106=CARTESIAN_POINT('Ctrl Pts',(18.1390363521672,-21.4419032627308,
6.39664100515899));
#146107=CARTESIAN_POINT('Ctrl Pts',(18.0573383986974,-21.4223814953014,
6.40081211913694));
#146108=CARTESIAN_POINT('Ctrl Pts',(17.9765415407097,-21.3988200192303,
6.4049832331149));
#146109=CARTESIAN_POINT('Ctrl Pts',(17.8970700591984,-21.3713280625392,
6.40915434709285));
#146110=CARTESIAN_POINT('Ctrl Pts',(17.8176252451101,-21.3438453310398,
6.41332406141322));
#146111=CARTESIAN_POINT('Ctrl Pts',(17.7395053586241,-21.3124348885695,
6.41749377573359));
#146112=CARTESIAN_POINT('Ctrl Pts',(17.6631189946706,-21.2772556574331,
6.42166349005396));
#146113=CARTESIAN_POINT('Ctrl Pts',(17.586735348872,-21.2420776781249,6.425833055998));
#146114=CARTESIAN_POINT('Ctrl Pts',(17.5120855204508,-21.2031313700068,
6.43000262194203));
#146115=CARTESIAN_POINT('Ctrl Pts',(17.4395563508726,-21.1606230188137,
6.43417218788607));
#146116=CARTESIAN_POINT('Ctrl Pts',(17.3644771451662,-21.1166201264322,
6.43848835062499));
#146117=CARTESIAN_POINT('Ctrl Pts',(17.2916709526712,-21.0688003143231,
6.44280451336392));
#146118=CARTESIAN_POINT('Ctrl Pts',(17.2215354755328,-21.0174420984933,
6.44712067610284));
#146119=CARTESIAN_POINT('Ctrl Pts',(17.1536846541854,-20.9677568711423,
6.45129624029452));
#146120=CARTESIAN_POINT('Ctrl Pts',(17.0883335592485,-20.9147605602812,
6.4554718044862));
#146121=CARTESIAN_POINT('Ctrl Pts',(17.0258081406203,-20.8587460689743,
6.45964736867787));
#146122=CARTESIAN_POINT('Ctrl Pts',(16.9601247117371,-20.7999024188732,
6.46403383069042));
#146123=CARTESIAN_POINT('Ctrl Pts',(16.8975603248983,-20.7377280904825,
6.46842029270297));
#146124=CARTESIAN_POINT('Ctrl Pts',(16.838447047551,-20.6726042556212,6.47280675471551));
#146125=CARTESIAN_POINT('Ctrl Pts',(16.7793337702036,-20.6074804207598,
6.47719321672806));
#146126=CARTESIAN_POINT('Ctrl Pts',(16.7236719107426,-20.5394075767508,
6.48157967874061));
#146127=CARTESIAN_POINT('Ctrl Pts',(16.6717415022696,-20.4688025212726,
6.48596614075316));
#146128=CARTESIAN_POINT('Ctrl Pts',(16.6219091295864,-20.4010499743281,
6.49017538570612));
#146129=CARTESIAN_POINT('Ctrl Pts',(16.5753265021952,-20.3307132360493,
6.49438463065908));
#146130=CARTESIAN_POINT('Ctrl Pts',(16.532270626113,-20.2581346654013,6.49859387561204));
#146131=CARTESIAN_POINT('Ctrl Pts',(16.489277141859,-20.1856612676153,6.50279702099133));
#146132=CARTESIAN_POINT('Ctrl Pts',(16.4498004872776,-20.110952875341,6.50700016637061));
#146133=CARTESIAN_POINT('Ctrl Pts',(16.4140760664827,-20.0343829926109,
6.5112033117499));
#146134=CARTESIAN_POINT('Ctrl Pts',(16.3783931208862,-19.9579020056842,
6.51540157737789));
#146135=CARTESIAN_POINT('Ctrl Pts',(16.3464539443372,-19.8795642299173,
6.51959984300589));
#146136=CARTESIAN_POINT('Ctrl Pts',(16.3184487740251,-19.7997689984254,
6.52379810863388));
#146137=CARTESIAN_POINT('Ctrl Pts',(16.2904693914727,-19.7200472440891,
6.52799250840909));
#146138=CARTESIAN_POINT('Ctrl Pts',(16.2664169618497,-19.6388711282231,
6.5321869081843));
#146139=CARTESIAN_POINT('Ctrl Pts',(16.2464336691667,-19.5566600282013,
6.53638130795952));
#146140=CARTESIAN_POINT('Ctrl Pts',(16.2264610773219,-19.4744929513394,
6.54057346167876));
#146141=CARTESIAN_POINT('Ctrl Pts',(16.210553397436,-19.3912924312907,6.54476561539801));
#146142=CARTESIAN_POINT('Ctrl Pts',(16.1988026788696,-19.3074919730929,
6.54895776911726));
#146143=CARTESIAN_POINT('Ctrl Pts',(16.1870533030452,-19.2237010906829,
6.55314944380363));
#146144=CARTESIAN_POINT('Ctrl Pts',(16.1794600117858,-19.1393108539568,
6.55734111849));
#146145=CARTESIAN_POINT('Ctrl Pts',(16.1760633700115,-19.0547628189716,
6.56153279317637));
#146146=CARTESIAN_POINT('Ctrl Pts',(16.1746649834927,-19.0199546642812,
6.56325849219375));
#146147=CARTESIAN_POINT('Ctrl Pts',(16.173977295445,-18.9851198216844,6.56498419121113));
#146148=CARTESIAN_POINT('Ctrl Pts',(16.1740005716256,-18.9502892333483,
6.5667098902285));
#146149=CARTESIAN_POINT('Ctrl Pts',(16.174000571626,-18.9502892327451,6.56670989025839));
#146150=CARTESIAN_POINT('Ctrl Pts',(16.1740643617891,-18.8548333601137,
6.57143929947809));
#146151=CARTESIAN_POINT('Ctrl Pts',(16.1794711562484,-18.7595846663132,
6.57616870869779));
#146152=CARTESIAN_POINT('Ctrl Pts',(16.1901275024526,-18.6650980721186,
6.58089811791749));
#146153=CARTESIAN_POINT('Ctrl Pts',(16.2008364140088,-18.5701453968694,
6.585650856246));
#146154=CARTESIAN_POINT('Ctrl Pts',(16.2168466650978,-18.4759625571763,
6.59040359457451));
#146155=CARTESIAN_POINT('Ctrl Pts',(16.2380139506878,-18.3830943473309,
6.59515633290303));
#146156=CARTESIAN_POINT('Ctrl Pts',(16.2593038089219,-18.2896883688619,
6.59993659274351));
#146157=CARTESIAN_POINT('Ctrl Pts',(16.2858104835345,-18.19761248234,6.604716852584));
#146158=CARTESIAN_POINT('Ctrl Pts',(16.3173390825673,-18.1073994967126,
6.60949711242449));
#146159=CARTESIAN_POINT('Ctrl Pts',(16.3253523527945,-18.0844710744544,
6.61071205742785));
#146160=CARTESIAN_POINT('Ctrl Pts',(16.333689786842,-18.0616628735359,6.61192700243122));
#146161=CARTESIAN_POINT('Ctrl Pts',(16.3423477078173,-18.0389833992214,
6.61314194743458));
#146162=CARTESIAN_POINT('Ctrl Pts',(16.3721681801721,-17.9608684985717,
6.61732658182763));
#146163=CARTESIAN_POINT('Ctrl Pts',(16.405875193857,-17.8840707367779,6.62151121622068));
#146164=CARTESIAN_POINT('Ctrl Pts',(16.4433319467771,-17.8090039939072,
6.62569585061373));
#146165=CARTESIAN_POINT('Ctrl Pts',(16.4807353846456,-17.7340440992537,
6.62987452869767));
#146166=CARTESIAN_POINT('Ctrl Pts',(16.5218777565726,-17.6608107375732,
6.63405320678161));
#146167=CARTESIAN_POINT('Ctrl Pts',(16.5665735905076,-17.5896994606788,
6.63823188486555));
#146168=CARTESIAN_POINT('Ctrl Pts',(16.6120705651436,-17.5173135652528,
6.64248546275099));
#146169=CARTESIAN_POINT('Ctrl Pts',(16.661249474465,-17.4471270300731,6.64673904063642));
#146170=CARTESIAN_POINT('Ctrl Pts',(16.7138648542455,-17.3795325145214,
6.65099261852186));
#146171=CARTESIAN_POINT('Ctrl Pts',(16.7654601822184,-17.3132484505536,
6.65516373249981));
#146172=CARTESIAN_POINT('Ctrl Pts',(16.8203596287512,-17.2494571801029,
6.65933484647777));
#146173=CARTESIAN_POINT('Ctrl Pts',(16.8782881026493,-17.1884996869773,
6.66350596045572));
#146174=CARTESIAN_POINT('Ctrl Pts',(16.9361971380885,-17.1275626487273,
6.66767567477609));
#146175=CARTESIAN_POINT('Ctrl Pts',(16.99713286563,-17.0694578324917,6.67184538909646));
#146176=CARTESIAN_POINT('Ctrl Pts',(17.060781453689,-17.0144913687209,6.67601510341684));
#146177=CARTESIAN_POINT('Ctrl Pts',(17.1244277768581,-16.9595268608928,
6.68018466936088));
#146178=CARTESIAN_POINT('Ctrl Pts',(17.1907864198799,-16.9077007835217,
6.68435423530492));
#146179=CARTESIAN_POINT('Ctrl Pts',(17.2595094445541,-16.8592798558094,
6.68852380124896));
#146180=CARTESIAN_POINT('Ctrl Pts',(17.3306486859969,-16.8091565080125,
6.69283996398789));
#146181=CARTESIAN_POINT('Ctrl Pts',(17.4043212347438,-16.7626825189769,
6.69715612672681));
#146182=CARTESIAN_POINT('Ctrl Pts',(17.4801089073792,-16.7201045885064,
6.70147228946573));
#146183=CARTESIAN_POINT('Ctrl Pts',(17.5534278045499,-16.6789136296426,
6.70564785365741));
#146184=CARTESIAN_POINT('Ctrl Pts',(17.6287256988455,-16.6413689670528,
6.70982341784909));
#146185=CARTESIAN_POINT('Ctrl Pts',(17.7056010183993,-16.6076460304292,
6.71399898204077));
#146186=CARTESIAN_POINT('Ctrl Pts',(17.78635912759,-16.5722198284453,6.71838544405331));
#146187=CARTESIAN_POINT('Ctrl Pts',(17.8688576552586,-16.5410117758975,
6.72277190606585));
#146188=CARTESIAN_POINT('Ctrl Pts',(17.9526121488767,-16.5141663251738,
6.72715836807839));
#146189=CARTESIAN_POINT('Ctrl Pts',(18.0363666424947,-16.48732087445,6.73154483009094));
#146190=CARTESIAN_POINT('Ctrl Pts',(18.1213765216826,-16.4648381003647,
6.73593129210348));
#146191=CARTESIAN_POINT('Ctrl Pts',(18.20714644876,-16.4468003401833,6.74031775411602));
#146192=CARTESIAN_POINT('Ctrl Pts',(18.2889699743511,-16.4295925240862,
6.74450238850907));
#146193=CARTESIAN_POINT('Ctrl Pts',(18.3717897057139,-16.4163656164704,
6.74868702290212));
#146194=CARTESIAN_POINT('Ctrl Pts',(18.4551835868307,-16.407228613854,6.75287165729516));
#146195=CARTESIAN_POINT('Ctrl Pts',(18.5384587670798,-16.3981046166299,
6.75705033537911));
#146196=CARTESIAN_POINT('Ctrl Pts',(18.6223060204197,-16.3930590108019,
6.76122901346306));
#146197=CARTESIAN_POINT('Ctrl Pts',(18.7062923578699,-16.3921499484213,
6.76540769154701));
#146198=CARTESIAN_POINT('Ctrl Pts',(18.7917840900589,-16.3912245917508,
6.76966126943244));
#146199=CARTESIAN_POINT('Ctrl Pts',(18.877419469749,-16.3945856314592,6.77391484731788));
#146200=CARTESIAN_POINT('Ctrl Pts',(18.9627354674095,-16.4022392100534,
6.77816842520332));
#146201=CARTESIAN_POINT('Ctrl Pts',(19.0463974479748,-16.4097444090919,
6.78233953918127));
#146202=CARTESIAN_POINT('Ctrl Pts',(19.1297518403943,-16.4213771508024,
6.78651065315922));
#146203=CARTESIAN_POINT('Ctrl Pts',(19.2123630296012,-16.4370906950924,
6.79068176713717));
#146204=CARTESIAN_POINT('Ctrl Pts',(19.2949464978256,-16.4527989665508,
6.79485148145754));
#146205=CARTESIAN_POINT('Ctrl Pts',(19.3767868065739,-16.472585235142,6.79902119577791));
#146206=CARTESIAN_POINT('Ctrl Pts',(19.457456677499,-16.4963513207745,6.80319091009829));
#146207=CARTESIAN_POINT('Ctrl Pts',(19.5381236778441,-16.5201165607077,
6.80736047604233));
#146208=CARTESIAN_POINT('Ctrl Pts',(19.6176198821352,-16.5478612052844,
6.81153004198638));
#146209=CARTESIAN_POINT('Ctrl Pts',(19.6955326893842,-16.579437063586,6.81569960793043));
#146210=CARTESIAN_POINT('Ctrl Pts',(19.7761848148201,-16.6121230901123,
6.82001577066935));
#146211=CARTESIAN_POINT('Ctrl Pts',(19.8551396382572,-16.6489145558588,
6.82433193340827));
#146212=CARTESIAN_POINT('Ctrl Pts',(19.9319633694499,-16.6895933686765,
6.82864809614719));
#146213=CARTESIAN_POINT('Ctrl Pts',(20.0062845756794,-16.7289470734454,
6.83282366033887));
#146214=CARTESIAN_POINT('Ctrl Pts',(20.0786110173904,-16.771938472629,6.83699922453055));
#146215=CARTESIAN_POINT('Ctrl Pts',(20.1485778227392,-16.8183248646023,
6.84117478872223));
#146216=CARTESIAN_POINT('Ctrl Pts',(20.2220784850958,-16.867054122961,6.84556125073476));
#146217=CARTESIAN_POINT('Ctrl Pts',(20.2929744068258,-16.9195300021186,
6.8499477127473));
#146218=CARTESIAN_POINT('Ctrl Pts',(20.3608819013655,-16.9754233435029,
6.85433417475984));
#146219=CARTESIAN_POINT('Ctrl Pts',(20.4287893959053,-17.0313166848872,
6.85872063677238));
#146220=CARTESIAN_POINT('Ctrl Pts',(20.4937080861994,-17.0906270409862,
6.86310709878492));
#146221=CARTESIAN_POINT('Ctrl Pts',(20.5553006227462,-17.1529824788,6.86749356079746));
#146222=CARTESIAN_POINT('Ctrl Pts',(20.6140591953844,-17.2124688504871,
6.87167819519051));
#146223=CARTESIAN_POINT('Ctrl Pts',(20.6700096812721,-17.2749476638323,
6.87586282958355));
#146224=CARTESIAN_POINT('Ctrl Pts',(20.7228319806688,-17.3401230342644,
6.8800474639766));
#146225=CARTESIAN_POINT('Ctrl Pts',(20.7755790940605,-17.4052056356238,
6.88422614206054));
#146226=CARTESIAN_POINT('Ctrl Pts',(20.8252065780214,-17.4729768158299,
6.88840482014449));
#146227=CARTESIAN_POINT('Ctrl Pts',(20.8714311671561,-17.5431039762745,
6.89258349822843));
#146228=CARTESIAN_POINT('Ctrl Pts',(20.9184842988301,-17.6144881156706,
6.89683707611387));
#146229=CARTESIAN_POINT('Ctrl Pts',(20.9620110031542,-17.6883131849442,
6.90109065399931));
#146230=CARTESIAN_POINT('Ctrl Pts',(21.0017554861493,-17.7641931743588,
6.90534423188474));
#146231=CARTESIAN_POINT('Ctrl Pts',(21.0407294447865,-17.838602082111,6.90951534586269));
#146232=CARTESIAN_POINT('Ctrl Pts',(21.0760663016048,-17.9149865174727,
6.91368645984064));
#146233=CARTESIAN_POINT('Ctrl Pts',(21.1075695674518,-17.9929548975847,
6.9178575738186));
#146234=CARTESIAN_POINT('Ctrl Pts',(21.1390622620736,-18.0708971146537,
6.92202728813897));
#146235=CARTESIAN_POINT('Ctrl Pts',(21.1667237483346,-18.1504217947136,
6.92619700245934));
#146236=CARTESIAN_POINT('Ctrl Pts',(21.1904053024889,-18.2311165212712,
6.93036671677971));
#146237=CARTESIAN_POINT('Ctrl Pts',(21.214086013952,-18.3118083763641,6.93453628272375));
#146238=CARTESIAN_POINT('Ctrl Pts',(21.2337869461661,-18.3936697535163,
6.9387058486678));
#146239=CARTESIAN_POINT('Ctrl Pts',(21.2494093711531,-18.4762735076587,
6.94287541461184));
#146240=CARTESIAN_POINT('Ctrl Pts',(21.2655810613302,-18.561781507894,6.94719157735076));
#146241=CARTESIAN_POINT('Ctrl Pts',(21.2773820094429,-18.6480845421362,
6.95150774008968));
#146242=CARTESIAN_POINT('Ctrl Pts',(21.2847607940422,-18.7346998122938,
6.9558239028286));
#146243=CARTESIAN_POINT('Ctrl Pts',(21.2918992155093,-18.8184935991363,
6.95999946702028));
#146244=CARTESIAN_POINT('Ctrl Pts',(21.2948991834511,-18.9025791196893,
6.96417503121196));
#146245=CARTESIAN_POINT('Ctrl Pts',(21.2937672733171,-18.9865182046883,
6.96835059540364));
#146246=CARTESIAN_POINT('Ctrl Pts',(21.2925781930931,-19.0746968533244,
6.97273705741618));
#146247=CARTESIAN_POINT('Ctrl Pts',(21.2868289009943,-19.1627133020808,
6.97712351942873));
#146248=CARTESIAN_POINT('Ctrl Pts',(21.2765884850301,-19.250066763985,6.98150998144127));
#146249=CARTESIAN_POINT('Ctrl Pts',(21.2663480690658,-19.3374202258893,
6.98589644345381));
#146250=CARTESIAN_POINT('Ctrl Pts',(21.2516167014297,-19.4241101416678,
6.99028290546635));
#146251=CARTESIAN_POINT('Ctrl Pts',(21.2325245180281,-19.5096515334976,
6.9946693674789));
#146252=CARTESIAN_POINT('Ctrl Pts',(21.2143148178506,-19.5912390117464,
6.99885307745113));
#146253=CARTESIAN_POINT('Ctrl Pts',(21.1920707686421,-19.6720854131111,
7.00303678742336));
#146254=CARTESIAN_POINT('Ctrl Pts',(21.1658678428317,-19.7517617113874,
7.00722049739559));
#146255=CARTESIAN_POINT('Ctrl Pts',(21.1396995424223,-19.8313327228036,
7.01139867887696));
#146256=CARTESIAN_POINT('Ctrl Pts',(21.1095828937122,-19.9097362679935,
7.01557686035833));
#146257=CARTESIAN_POINT('Ctrl Pts',(21.0756441740988,-19.9865542817607,
7.0197550418397));
#146258=CARTESIAN_POINT('Ctrl Pts',(21.0417401170689,-20.0632938390966,
7.02392895602501));
#146259=CARTESIAN_POINT('Ctrl Pts',(21.0040219265316,-20.1384506626217,
7.02810287021032));
#146260=CARTESIAN_POINT('Ctrl Pts',(20.9626649802985,-20.2116239143455,
7.03227678439562));
#146261=CARTESIAN_POINT('Ctrl Pts',(20.9205833380602,-20.2860793778389,
7.0365238379012));
#146262=CARTESIAN_POINT('Ctrl Pts',(20.8747343561323,-20.3584806290068,
7.04077089140678));
#146263=CARTESIAN_POINT('Ctrl Pts',(20.8253528363596,-20.4284292444444,
7.04501794491235));
#146264=CARTESIAN_POINT('Ctrl Pts',(20.7768706609689,-20.4971039441618,
7.04918765037907));
#146265=CARTESIAN_POINT('Ctrl Pts',(20.7249838359412,-20.5634142202303,
7.05335735584579));
#146266=CARTESIAN_POINT('Ctrl Pts',(20.6699585837801,-20.6270117497762,
7.0575270613125));
#146267=CARTESIAN_POINT('Ctrl Pts',(20.613402253929,-20.6923788806378,7.06181278883751));
#146268=CARTESIAN_POINT('Ctrl Pts',(20.5535305486344,-20.754879647566,7.06609851636252));
#146269=CARTESIAN_POINT('Ctrl Pts',(20.4906759641957,-20.8141733423119,
7.07038424388752));
#146270=CARTESIAN_POINT('Ctrl Pts',(20.427821379757,-20.8734670370578,7.07466997141253));
#146271=CARTESIAN_POINT('Ctrl Pts',(20.3619843152027,-20.9295533148579,
7.07895569893754));
#146272=CARTESIAN_POINT('Ctrl Pts',(20.2935357468249,-20.9821350335323,
7.08324142646255));
#146273=CARTESIAN_POINT('Origin',(18.734,-18.952,-1.76670989022851));
#146274=CARTESIAN_POINT('',(20.290984793813,-20.9788230549133,7.94987222229573));
#146275=CARTESIAN_POINT('',(20.2961055615655,-20.9854720348211,7.88329696296241));
#146276=CARTESIAN_POINT('',(20.2935357468249,-20.9821350335323,-1.76670989022851));
#146277=CARTESIAN_POINT('',(16.1743644997381,-18.9525601738959,7.4332900849458));
#146278=CARTESIAN_POINT('Ctrl Pts',(16.1781030393919,-18.952558854618,7.43329010977151));
#146279=CARTESIAN_POINT('Ctrl Pts',(16.1790025482941,-18.4906083143692,
7.4561794192865));
#146280=CARTESIAN_POINT('Ctrl Pts',(16.5197425194489,-17.1718695770502,
7.52146066436197));
#146281=CARTESIAN_POINT('Ctrl Pts',(18.6352034714368,-15.9265199028681,
7.62913384499793));
#146282=CARTESIAN_POINT('Ctrl Pts',(21.2244732819954,-17.231292760559,7.75630965167936));
#146283=CARTESIAN_POINT('Ctrl Pts',(21.4803857440547,-19.6552910993149,
7.86322244411196));
#146284=CARTESIAN_POINT('Ctrl Pts',(20.6448527398538,-20.7063099546061,
7.92774330098409));
#146285=CARTESIAN_POINT('Ctrl Pts',(20.290984793813,-20.9788230549133,7.94987222229573));
#146286=CARTESIAN_POINT('Ctrl Pts',(20.2935357468249,-20.9821350335323,
7.14996297925329));
#146287=CARTESIAN_POINT('Ctrl Pts',(20.2269740650341,-21.0332672589297,
7.15413571584543));
#146288=CARTESIAN_POINT('Ctrl Pts',(20.1578294177455,-21.0811729380824,
7.15830845243758));
#146289=CARTESIAN_POINT('Ctrl Pts',(20.0864499467968,-21.1255866997683,
7.16248118902972));
#146290=CARTESIAN_POINT('Ctrl Pts',(20.015108654789,-21.1699767057388,7.16665169373835));
#146291=CARTESIAN_POINT('Ctrl Pts',(19.9415353022569,-21.210878260028,7.17082219844698));
#146292=CARTESIAN_POINT('Ctrl Pts',(19.8661075037954,-21.2480689449252,
7.17499270315561));
#146293=CARTESIAN_POINT('Ctrl Pts',(19.7906974228729,-21.2852508939529,
7.17916222823762));
#146294=CARTESIAN_POINT('Ctrl Pts',(19.7134341737692,-21.3187235017973,
7.18333175331963));
#146295=CARTESIAN_POINT('Ctrl Pts',(19.634719278428,-21.3483106604671,7.18750127840164));
#146296=CARTESIAN_POINT('Ctrl Pts',(19.5559992603542,-21.3778997446568,
7.1916710748346));
#146297=CARTESIAN_POINT('Ctrl Pts',(19.4758278395417,-21.4036027169435,
7.19584087126757));
#146298=CARTESIAN_POINT('Ctrl Pts',(19.3946244955917,-21.4252923959419,
7.20001066770053));
#146299=CARTESIAN_POINT('Ctrl Pts',(19.3133366948555,-21.4470046336245,
7.20418480099438));
#146300=CARTESIAN_POINT('Ctrl Pts',(19.2310152730944,-21.4646951235253,
7.20835893428822));
#146301=CARTESIAN_POINT('Ctrl Pts',(19.1480923087683,-21.4782873074571,
7.21253306758207));
#146302=CARTESIAN_POINT('Ctrl Pts',(19.0651253024502,-21.4918867104611,
7.21670941783893));
#146303=CARTESIAN_POINT('Ctrl Pts',(18.9815565747079,-21.5013834208329,
7.22088576809579));
#146304=CARTESIAN_POINT('Ctrl Pts',(18.8978233448839,-21.5067528083302,
7.22506211835265));
#146305=CARTESIAN_POINT('Ctrl Pts',(18.8139435125698,-21.5121315967019,
7.22924578068082));
#146306=CARTESIAN_POINT('Ctrl Pts',(18.7298990634063,-21.5133686206996,
7.233429443009));
#146307=CARTESIAN_POINT('Ctrl Pts',(18.6461270483911,-21.5104914196408,
7.23761310533717));
#146308=CARTESIAN_POINT('Ctrl Pts',(18.5794262764124,-21.5082005408583,
7.24094421187599));
#146309=CARTESIAN_POINT('Ctrl Pts',(18.5128982522666,-21.5033024356435,
7.24427531841481));
#146310=CARTESIAN_POINT('Ctrl Pts',(18.4467595506041,-21.4958342957494,
7.24760642495362));
#146311=CARTESIAN_POINT('Ctrl Pts',(18.3636741606704,-21.4864525978996,
7.25179105934667));
#146312=CARTESIAN_POINT('Ctrl Pts',(18.2808942658294,-21.4729786230522,
7.25597569373971));
#146313=CARTESIAN_POINT('Ctrl Pts',(18.1988547913486,-21.4554415522751,
7.26016032813276));
#146314=CARTESIAN_POINT('Ctrl Pts',(18.1169320899054,-21.4379294433476,
7.2643390062167));
#146315=CARTESIAN_POINT('Ctrl Pts',(18.0357481614735,-21.4163658213153,
7.26851768430064));
#146316=CARTESIAN_POINT('Ctrl Pts',(17.9557323296064,-21.3908315713104,
7.27269636238458));
#146317=CARTESIAN_POINT('Ctrl Pts',(17.8742822714594,-21.3648396382252,
7.27694994027001));
#146318=CARTESIAN_POINT('Ctrl Pts',(17.7940430771268,-21.3347333841336,
7.28120351815545));
#146319=CARTESIAN_POINT('Ctrl Pts',(17.7154562415199,-21.3006525098578,
7.28545709604089));
#146320=CARTESIAN_POINT('Ctrl Pts',(17.638392965071,-21.2672323598332,7.28962821001883));
#146321=CARTESIAN_POINT('Ctrl Pts',(17.5629189921772,-21.229990517358,7.29379932399678));
#146322=CARTESIAN_POINT('Ctrl Pts',(17.4894331713725,-21.1891082694139,
7.29797043797473));
#146323=CARTESIAN_POINT('Ctrl Pts',(17.4159720094446,-21.1482397399029,
7.30214015229511));
#146324=CARTESIAN_POINT('Ctrl Pts',(17.3444980763224,-21.1037334544496,
7.30630986661548));
#146325=CARTESIAN_POINT('Ctrl Pts',(17.275386138507,-21.0558169129134,7.31047958093586));
#146326=CARTESIAN_POINT('Ctrl Pts',(17.2062766599911,-21.0079020764535,
7.3146491468799));
#146327=CARTESIAN_POINT('Ctrl Pts',(17.1395293872401,-20.9565774880024,
7.31881871282395));
#146328=CARTESIAN_POINT('Ctrl Pts',(17.0754894346058,-20.9021135106644,
7.32298827876799));
#146329=CARTESIAN_POINT('Ctrl Pts',(17.0091979162386,-20.8457346470717,
7.32730444150691));
#146330=CARTESIAN_POINT('Ctrl Pts',(16.9458080406879,-20.7859918669771,
7.33162060424583));
#146331=CARTESIAN_POINT('Ctrl Pts',(16.8856630675041,-20.7232285521558,
7.33593676698475));
#146332=CARTESIAN_POINT('Ctrl Pts',(16.8274773104958,-20.6625097457132,
7.34011233117643));
#146333=CARTESIAN_POINT('Ctrl Pts',(16.77232857006,-20.5989645570467,7.34428789536811));
#146334=CARTESIAN_POINT('Ctrl Pts',(16.7204869451087,-20.532938068927,7.34846345955978));
#146335=CARTESIAN_POINT('Ctrl Pts',(16.6660269229229,-20.4635767398552,
7.35284992157233));
#146336=CARTESIAN_POINT('Ctrl Pts',(16.6152172172817,-20.3914773402462,
7.35723638358488));
#146337=CARTESIAN_POINT('Ctrl Pts',(16.5683186145659,-20.317072941928,7.36162284559742));
#146338=CARTESIAN_POINT('Ctrl Pts',(16.52142001185,-20.2426685436099,7.36600930760997));
#146339=CARTESIAN_POINT('Ctrl Pts',(16.4784327293519,-20.1659596899256,
7.37039576962251));
#146340=CARTESIAN_POINT('Ctrl Pts',(16.4395601204679,-20.0874054955004,
7.37478223163505));
#146341=CARTESIAN_POINT('Ctrl Pts',(16.3997963941391,-20.0070505211682,
7.37926924910123));
#146342=CARTESIAN_POINT('Ctrl Pts',(16.3642056179145,-19.9244993534859,
7.38375626656741));
#146343=CARTESIAN_POINT('Ctrl Pts',(16.333017909016,-19.8401919830611,7.38824328403359));
#146344=CARTESIAN_POINT('Ctrl Pts',(16.3019356806124,-19.7561697500662,
7.39271512587963));
#146345=CARTESIAN_POINT('Ctrl Pts',(16.2752269677052,-19.6704034844248,
7.39718696772568));
#146346=CARTESIAN_POINT('Ctrl Pts',(16.2530742870064,-19.5833537887801,
7.40165880957172));
#146347=CARTESIAN_POINT('Ctrl Pts',(16.2309688572623,-19.4964897673338,
7.40612111312307));
#146348=CARTESIAN_POINT('Ctrl Pts',(16.2134002030054,-19.408348109083,7.41058341667443));
#146349=CARTESIAN_POINT('Ctrl Pts',(16.2005019648758,-19.3194067310513,
7.41504572022578));
#146350=CARTESIAN_POINT('Ctrl Pts',(16.1876417930136,-19.2307278436206,
7.41949485428542));
#146351=CARTESIAN_POINT('Ctrl Pts',(16.1794246278367,-19.1412542906273,
7.42394398834506));
#146352=CARTESIAN_POINT('Ctrl Pts',(16.175933399183,-19.0514749505386,7.4283931224047));
#146353=CARTESIAN_POINT('Ctrl Pts',(16.1746525201579,-19.0185362676236,
7.43002544244505));
#146354=CARTESIAN_POINT('Ctrl Pts',(16.1740072831437,-18.9855565464226,
7.4316577624854));
#146355=CARTESIAN_POINT('Ctrl Pts',(16.1740000613162,-18.952560302501,7.43329008252576));
#146356=CARTESIAN_POINT('',(16.1738764939443,-18.9508698166505,7.36670989022851));
#146357=CARTESIAN_POINT('Ctrl Pts',(20.2935357468249,-20.9821350335323,
7.08324142646255));
#146358=CARTESIAN_POINT('Ctrl Pts',(20.226845872581,-21.033365735489,7.08741703796854));
#146359=CARTESIAN_POINT('Ctrl Pts',(20.1576775032969,-21.0812695904658,
7.09159264947453));
#146360=CARTESIAN_POINT('Ctrl Pts',(20.0864031447847,-21.1256158202351,
7.09576826098051));
#146361=CARTESIAN_POINT('Ctrl Pts',(20.012217792683,-21.1717732426027,7.10011441317715));
#146362=CARTESIAN_POINT('Ctrl Pts',(19.9357512244538,-21.2140759358748,
7.10446056537378));
#146363=CARTESIAN_POINT('Ctrl Pts',(19.8574497188556,-21.2523175279085,
7.10880671757042));
#146364=CARTESIAN_POINT('Ctrl Pts',(19.7791482132574,-21.2905591199422,
7.11315286976705));
#146365=CARTESIAN_POINT('Ctrl Pts',(19.6990123085245,-21.3247394606782,
7.11749902196369));
#146366=CARTESIAN_POINT('Ctrl Pts',(19.6175072439402,-21.3547099179687,
7.12184517416032));
#146367=CARTESIAN_POINT('Ctrl Pts',(19.5390311848803,-21.3835665710906,
7.12602980855337));
#146368=CARTESIAN_POINT('Ctrl Pts',(19.4589938470389,-21.4086281659991,
7.13021444294642));
#146369=CARTESIAN_POINT('Ctrl Pts',(19.3777970941006,-21.429725832619,7.13439907733946));
#146370=CARTESIAN_POINT('Ctrl Pts',(19.29671591469,-21.4507934693218,7.13857775542341));
#146371=CARTESIAN_POINT('Ctrl Pts',(19.2144790396055,-21.4679082701427,
7.14275643350735));
#146372=CARTESIAN_POINT('Ctrl Pts',(19.1315065014625,-21.4809500946628,
7.1469351115913));
#146373=CARTESIAN_POINT('Ctrl Pts',(19.0470467402046,-21.4942256845144,
7.15118868947673));
#146374=CARTESIAN_POINT('Ctrl Pts',(18.9618251354748,-21.5032806792605,
7.15544226736217));
#146375=CARTESIAN_POINT('Ctrl Pts',(18.8762989641011,-21.508042058499,7.1596958452476));
#146376=CARTESIAN_POINT('Ctrl Pts',(18.79243088445,-21.5127111291099,7.16386695922556));
#146377=CARTESIAN_POINT('Ctrl Pts',(18.7082704224838,-21.5132515520536,
7.16803807320351));
#146378=CARTESIAN_POINT('Ctrl Pts',(18.6242553740811,-21.5096465973785,
7.17220918718146));
#146379=CARTESIAN_POINT('Ctrl Pts',(18.5402685177393,-21.5060428523808,
7.17637890150183));
#146380=CARTESIAN_POINT('Ctrl Pts',(18.456427437281,-21.4982965120596,7.18054861582221));
#146381=CARTESIAN_POINT('Ctrl Pts',(18.3731691163824,-21.4864429513066,
7.18471833014258));
#146382=CARTESIAN_POINT('Ctrl Pts',(18.2899137581722,-21.4745898123542,
7.18888789608662));
#146383=CARTESIAN_POINT('Ctrl Pts',(18.2072415736112,-21.4586298092437,
7.19305746203067));
#146384=CARTESIAN_POINT('Ctrl Pts',(18.1255822535273,-21.4386499242509,
7.19722702797471));
#146385=CARTESIAN_POINT('Ctrl Pts',(18.0410518924869,-21.4179675711496,
7.20154319071364));
#146386=CARTESIAN_POINT('Ctrl Pts',(17.9576074580675,-21.3929775239273,
7.20585935345255));
#146387=CARTESIAN_POINT('Ctrl Pts',(17.8757097136974,-21.363832868264,7.21017551619147));
#146388=CARTESIAN_POINT('Ctrl Pts',(17.7964797797361,-21.3356375966935,
7.21435108038315));
#146389=CARTESIAN_POINT('Ctrl Pts',(17.7186977338733,-21.303554456016,7.21852664457484));
#146390=CARTESIAN_POINT('Ctrl Pts',(17.6427597031132,-21.2677708467054,
7.22270220876652));
#146391=CARTESIAN_POINT('Ctrl Pts',(17.562986222945,-21.2301798923558,7.22708867077906));
#146392=CARTESIAN_POINT('Ctrl Pts',(17.4852484504759,-21.1885050997006,
7.2314751327916));
#146393=CARTESIAN_POINT('Ctrl Pts',(17.4099736292609,-21.1430166976971,
7.23586159480414));
#146394=CARTESIAN_POINT('Ctrl Pts',(17.334698808046,-21.0975282956936,7.24024805681668));
#146395=CARTESIAN_POINT('Ctrl Pts',(17.2618873758782,-21.0482266726393,
7.24463451882922));
#146396=CARTESIAN_POINT('Ctrl Pts',(17.1919269101811,-20.9954310816997,
7.24902098084176));
#146397=CARTESIAN_POINT('Ctrl Pts',(17.1258771580207,-20.9455867065661,
7.25316224442402));
#146398=CARTESIAN_POINT('Ctrl Pts',(17.0621112325388,-20.892434299838,7.25730350800628));
#146399=CARTESIAN_POINT('Ctrl Pts',(17.0009846311415,-20.8362127616859,
7.26144477158854));
#146400=CARTESIAN_POINT('Ctrl Pts',(16.9399453026366,-20.7800714932715,
7.26558012252322));
#146401=CARTESIAN_POINT('Ctrl Pts',(16.8815381604268,-20.7208701082194,
7.26971547345791));
#146402=CARTESIAN_POINT('Ctrl Pts',(16.8260879518442,-20.6588894564388,
7.27385082439259));
#146403=CARTESIAN_POINT('Ctrl Pts',(16.770701311821,-20.5969798597695,7.27798143452813));
#146404=CARTESIAN_POINT('Ctrl Pts',(16.7182651826551,-20.5322976752766,
7.28211204466367));
#146405=CARTESIAN_POINT('Ctrl Pts',(16.6690684130046,-20.4651614391824,
7.2862426547992));
#146406=CARTESIAN_POINT('Ctrl Pts',(16.6199019406792,-20.3980665482496,
7.29037072114092));
#146407=CARTESIAN_POINT('Ctrl Pts',(16.5739711466917,-20.3285209831314,
7.29449878748264));
#146408=CARTESIAN_POINT('Ctrl Pts',(16.5315246255303,-20.2568763255016,
7.29862685382436));
#146409=CARTESIAN_POINT('Ctrl Pts',(16.4890908665707,-20.185253208944,7.30275367899921));
#146410=CARTESIAN_POINT('Ctrl Pts',(16.4501395400175,-20.1115326575802,
7.30688050417406));
#146411=CARTESIAN_POINT('Ctrl Pts',(16.4148750854128,-20.0360939214575,
7.31100732934891));
#146412=CARTESIAN_POINT('Ctrl Pts',(16.3796101195077,-19.9606540915462,
7.31513421435872));
#146413=CARTESIAN_POINT('Ctrl Pts',(16.3480323287909,-19.8834964546655,
7.31926109936854));
#146414=CARTESIAN_POINT('Ctrl Pts',(16.320298833946,-19.8050220870468,7.32338798437836));
#146415=CARTESIAN_POINT('Ctrl Pts',(16.2925397363851,-19.7264752742868,
7.32751867920247));
#146416=CARTESIAN_POINT('Ctrl Pts',(16.2686321752694,-19.646609748954,7.33164937402659));
#146417=CARTESIAN_POINT('Ctrl Pts',(16.2486837569799,-19.5658429540043,
7.3357800688507));
#146418=CARTESIAN_POINT('Ctrl Pts',(16.2287250388403,-19.4850344572077,
7.33991289645232));
#146419=CARTESIAN_POINT('Ctrl Pts',(16.2127296214478,-19.4033242264923,
7.34404572405394));
#146420=CARTESIAN_POINT('Ctrl Pts',(16.2007537416511,-19.3211387199432,
7.34817855165555));
#146421=CARTESIAN_POINT('Ctrl Pts',(16.1887593096482,-19.2388258972814,
7.35231778154836));
#146422=CARTESIAN_POINT('Ctrl Pts',(16.180796886798,-19.1560367972438,7.35645701144116));
#146423=CARTESIAN_POINT('Ctrl Pts',(16.176870697397,-19.0732011954116,7.36059624133396));
#146424=CARTESIAN_POINT('Ctrl Pts',(16.1749377014765,-19.0324184251309,
7.36263412429881));
#146425=CARTESIAN_POINT('Ctrl Pts',(16.1739822581149,-18.9916243590029,
7.36467200726366));
#146426=CARTESIAN_POINT('Ctrl Pts',(16.1740002494514,-18.9508698712832,
7.36670989022851));
#146427=CARTESIAN_POINT('Ctrl Pts',(16.170378839146,-18.9508682725878,7.36670989022851));
#146428=CARTESIAN_POINT('Ctrl Pts',(16.1700290602903,-18.8875375837258,
7.36987218932674));
#146429=CARTESIAN_POINT('Ctrl Pts',(16.2008981559486,-17.9755793377669,
7.41542642398544));
#146430=CARTESIAN_POINT('Ctrl Pts',(17.2895132774888,-16.291783852743,7.50337259420463));
#146431=CARTESIAN_POINT('Ctrl Pts',(20.1889475254729,-16.2974907158275,
7.63054840088606));
#146432=CARTESIAN_POINT('Ctrl Pts',(21.746983751553,-18.7282885913632,7.75718985713872));
#146433=CARTESIAN_POINT('Ctrl Pts',(20.9598514166904,-20.4743156438175,
7.8414393778309));
#146434=CARTESIAN_POINT('Ctrl Pts',(20.2961055615625,-20.9854720348234,
7.8832969629626));
#146435=CARTESIAN_POINT('Origin',(18.734,-18.952,-1.76670989022851));
#146436=CARTESIAN_POINT('',(20.2935357468249,-20.9821350335323,8.74981199600226));
#146437=CARTESIAN_POINT('',(20.2935357468249,-20.9821350335323,8.68337763131693));
#146438=CARTESIAN_POINT('',(20.2935357468249,-20.9821350335323,-1.76670989022851));
#146439=CARTESIAN_POINT('',(16.1740010826189,-18.9496456407634,8.23329012251336));
#146440=CARTESIAN_POINT('Ctrl Pts',(16.1740010826189,-18.9496456407634,
8.23329012251336));
#146441=CARTESIAN_POINT('Ctrl Pts',(16.1741014808467,-18.8404782076363,
8.23871812867226));
#146442=CARTESIAN_POINT('Ctrl Pts',(16.1811885397045,-18.7316228555833,
8.24414613483116));
#146443=CARTESIAN_POINT('Ctrl Pts',(16.1951208364064,-18.6238345041446,
8.24957414099005));
#146444=CARTESIAN_POINT('Ctrl Pts',(16.2083299266979,-18.5216412981712,
8.25472038679507));
#146445=CARTESIAN_POINT('Ctrl Pts',(16.2276915596983,-18.4204066645004,
8.25986663260008));
#146446=CARTESIAN_POINT('Ctrl Pts',(16.253046772176,-18.32075434152,8.2650128784051));
#146447=CARTESIAN_POINT('Ctrl Pts',(16.2736641888711,-18.2397227402536,
8.26919751279815));
#146448=CARTESIAN_POINT('Ctrl Pts',(16.2982940662941,-18.1595514977397,
8.27338214719119));
#146449=CARTESIAN_POINT('Ctrl Pts',(16.3268482220626,-18.0806675043515,
8.27756678158424));
#146450=CARTESIAN_POINT('Ctrl Pts',(16.3553617345247,-18.0018957925641,
8.28174545966818));
#146451=CARTESIAN_POINT('Ctrl Pts',(16.3877882750862,-17.9244081193637,
8.28592413775211));
#146452=CARTESIAN_POINT('Ctrl Pts',(16.4239892031398,-17.8486187792113,
8.29010281583605));
#146453=CARTESIAN_POINT('Ctrl Pts',(16.4608390068116,-17.7714709696053,
8.29435639372149));
#146454=CARTESIAN_POINT('Ctrl Pts',(16.5015997218016,-17.6960834444033,
8.29860997160693));
#146455=CARTESIAN_POINT('Ctrl Pts',(16.5460727818104,-17.6228745401938,
8.30286354949236));
#146456=CARTESIAN_POINT('Ctrl Pts',(16.5896836447689,-17.5510849334478,
8.30703466347031));
#146457=CARTESIAN_POINT('Ctrl Pts',(16.636863945312,-17.4813906391621,8.31120577744826));
#146458=CARTESIAN_POINT('Ctrl Pts',(16.6873797310321,-17.4141620778998,
8.31537689142621));
#146459=CARTESIAN_POINT('Ctrl Pts',(16.7378785656923,-17.3469560758304,
8.31954660574659));
#146460=CARTESIAN_POINT('Ctrl Pts',(16.7917103865527,-17.2822145310262,
8.32371632006696));
#146461=CARTESIAN_POINT('Ctrl Pts',(16.8485987415143,-17.220277708609,8.32788603438733));
#146462=CARTESIAN_POINT('Ctrl Pts',(16.9054850721441,-17.1583430901697,
8.33205560033138));
#146463=CARTESIAN_POINT('Ctrl Pts',(16.9654274088045,-17.0992133339122,
8.33622516627543));
#146464=CARTESIAN_POINT('Ctrl Pts',(17.0281108772058,-17.0431934878746,
8.34039473221947));
#146465=CARTESIAN_POINT('Ctrl Pts',(17.0929982190277,-16.9852040531583,
8.34471089495839));
#146466=CARTESIAN_POINT('Ctrl Pts',(17.160822642128,-16.9305476379184,8.34902705769731));
#146467=CARTESIAN_POINT('Ctrl Pts',(17.2311971876102,-16.8795175013831,
8.35334322043624));
#146468=CARTESIAN_POINT('Ctrl Pts',(17.2992792896754,-16.8301496661781,
8.35751878462792));
#146469=CARTESIAN_POINT('Ctrl Pts',(17.3697475047294,-16.7841757035315,
8.36169434881959));
#146470=CARTESIAN_POINT('Ctrl Pts',(17.4422231594134,-16.7418161628217,
8.36586991301127));
#146471=CARTESIAN_POINT('Ctrl Pts',(17.518359387121,-16.6973171424109,8.37025637502381));
#146472=CARTESIAN_POINT('Ctrl Pts',(17.5967106568091,-16.6568075367651,
8.37464283703635));
#146473=CARTESIAN_POINT('Ctrl Pts',(17.6768123961764,-16.6204866780733,
8.3790292990489));
#146474=CARTESIAN_POINT('Ctrl Pts',(17.7569141355437,-16.5841658193815,
8.38341576106144));
#146475=CARTESIAN_POINT('Ctrl Pts',(17.8387657767031,-16.5520338488593,
8.38780222307398));
#146476=CARTESIAN_POINT('Ctrl Pts',(17.921884774769,-16.524229652346,8.39218868508653));
#146477=CARTESIAN_POINT('Ctrl Pts',(18.001179344522,-16.49770476813,8.39637331947957));
#146478=CARTESIAN_POINT('Ctrl Pts',(18.0819223576085,-16.4750194242753,
8.40055795387262));
#146479=CARTESIAN_POINT('Ctrl Pts',(18.1637071353304,-16.4563305410157,
8.40474258826567));
#146480=CARTESIAN_POINT('Ctrl Pts',(18.2453755025443,-16.4376682590682,
8.40892126634961));
#146481=CARTESIAN_POINT('Ctrl Pts',(18.3280822444037,-16.4229912402357,
8.41309994443356));
#146482=CARTESIAN_POINT('Ctrl Pts',(18.4114039612995,-16.4124071594418,
8.4172786225175));
#146483=CARTESIAN_POINT('Ctrl Pts',(18.4962191600883,-16.4016333666062,
8.42153220040294));
#146484=CARTESIAN_POINT('Ctrl Pts',(18.5816711403846,-16.3951008398354,
8.42578577828838));
#146485=CARTESIAN_POINT('Ctrl Pts',(18.667300667149,-16.3928690539566,8.43003935617381));
#146486=CARTESIAN_POINT('Ctrl Pts',(18.7512700984448,-16.3906805356019,
8.43421047015176));
#146487=CARTESIAN_POINT('Ctrl Pts',(18.8354097724167,-16.3926275022743,
8.43838158412972));
#146488=CARTESIAN_POINT('Ctrl Pts',(18.9192815899905,-16.3987137386477,
8.44255269810767));
#146489=CARTESIAN_POINT('Ctrl Pts',(19.0031252635658,-16.4047979327256,
8.44672241242804));
#146490=CARTESIAN_POINT('Ctrl Pts',(19.086700800805,-16.4150186047168,8.45089212674841));
#146491=CARTESIAN_POINT('Ctrl Pts',(19.1695724543109,-16.4293274812125,
8.45506184106879));
#146492=CARTESIAN_POINT('Ctrl Pts',(19.2524411588877,-16.443635848537,8.45923140701283));
#146493=CARTESIAN_POINT('Ctrl Pts',(19.3346055763513,-16.4620320520102,
8.46340097295687));
#146494=CARTESIAN_POINT('Ctrl Pts',(19.4156387740957,-16.484416448902,8.46757053890091));
#146495=CARTESIAN_POINT('Ctrl Pts',(19.4995209991075,-16.5075878535744,
8.47188670163983));
#146496=CARTESIAN_POINT('Ctrl Pts',(19.5821904685913,-16.5350329790257,
8.47620286437876));
#146497=CARTESIAN_POINT('Ctrl Pts',(19.6631911444339,-16.5665851897195,
8.48051902711768));
#146498=CARTESIAN_POINT('Ctrl Pts',(19.7415532317808,-16.5971095904687,
8.48469459130936));
#146499=CARTESIAN_POINT('Ctrl Pts',(19.8183531671026,-16.6314773734769,
8.48887015550104));
#146500=CARTESIAN_POINT('Ctrl Pts',(19.8932005345678,-16.6694895135711,
8.49304571969272));
#146501=CARTESIAN_POINT('Ctrl Pts',(19.971828264631,-16.7094215564963,8.49743218170526));
#146502=CARTESIAN_POINT('Ctrl Pts',(20.0483004884278,-16.7533754937361,
8.5018186437178));
#146503=CARTESIAN_POINT('Ctrl Pts',(20.122198134957,-16.8010685882386,8.50620510573035));
#146504=CARTESIAN_POINT('Ctrl Pts',(20.1960957814862,-16.8487616827411,
8.51059156774289));
#146505=CARTESIAN_POINT('Ctrl Pts',(20.2674184246211,-16.9001935334404,
8.51497802975543));
#146506=CARTESIAN_POINT('Ctrl Pts',(20.3357880909559,-16.9550335727229,
8.51936449176797));
#146507=CARTESIAN_POINT('Ctrl Pts',(20.4010119675945,-17.0073503405056,
8.52354912616102));
#146508=CARTESIAN_POINT('Ctrl Pts',(20.4637914133142,-17.0629632902855,
8.52773376055407));
#146509=CARTESIAN_POINT('Ctrl Pts',(20.5237743555655,-17.1216154075823,
8.53191839494712));
#146510=CARTESIAN_POINT('Ctrl Pts',(20.5836719195229,-17.1801840408498,
8.53609707303107));
#146511=CARTESIAN_POINT('Ctrl Pts',(20.6407805603835,-17.2417829302056,
8.54027575111501));
#146512=CARTESIAN_POINT('Ctrl Pts',(20.6947805623984,-17.3061143459765,
8.54445442919895));
#146513=CARTESIAN_POINT('Ctrl Pts',(20.7497484756404,-17.3715988561409,
8.54870800708439));
#146514=CARTESIAN_POINT('Ctrl Pts',(20.8014948330692,-17.4399145156592,
8.55296158496982));
#146515=CARTESIAN_POINT('Ctrl Pts',(20.8497210505507,-17.5107073731346,
8.55721516285526));
#146516=CARTESIAN_POINT('Ctrl Pts',(20.8970123087006,-17.5801277729269,
8.56138627683321));
#146517=CARTESIAN_POINT('Ctrl Pts',(20.9409184275291,-17.6519297794778,
8.56555739081116));
#146518=CARTESIAN_POINT('Ctrl Pts',(20.9811990900048,-17.7257470693688,
8.56972850478911));
#146519=CARTESIAN_POINT('Ctrl Pts',(21.0214662359151,-17.7995395891551,
8.57389821910949));
#146520=CARTESIAN_POINT('Ctrl Pts',(21.058110121399,-17.8753456457563,8.57806793342986));
#146521=CARTESIAN_POINT('Ctrl Pts',(21.0909354749525,-17.9527727150891,
8.58223764775023));
#146522=CARTESIAN_POINT('Ctrl Pts',(21.123759660439,-18.0301970292345,8.58640721369427));
#146523=CARTESIAN_POINT('Ctrl Pts',(21.152765405382,-18.1092418175489,8.59057677963832));
#146524=CARTESIAN_POINT('Ctrl Pts',(21.1778054030264,-18.1894941625543,
8.59474634558237));
#146525=CARTESIAN_POINT('Ctrl Pts',(21.2037257760979,-18.272568081008,8.59906250832129));
#146526=CARTESIAN_POINT('Ctrl Pts',(21.2253961847597,-18.3569355479854,
8.6033786710602));
#146527=CARTESIAN_POINT('Ctrl Pts',(21.2427098983461,-18.4421229109477,
8.60769483379912));
#146528=CARTESIAN_POINT('Ctrl Pts',(21.2594596195335,-18.5245353045217,
8.6118703979908));
#146529=CARTESIAN_POINT('Ctrl Pts',(21.2721321012068,-18.6077145253799,
8.61604596218248));
#146530=CARTESIAN_POINT('Ctrl Pts',(21.2806833673555,-18.6912245670412,
8.62022152637416));
#146531=CARTESIAN_POINT('Ctrl Pts',(21.2896665376286,-18.7789525023805,
8.6246079883867));
#146532=CARTESIAN_POINT('Ctrl Pts',(21.2941011966021,-18.8670449731774,
8.62899445039924));
#146533=CARTESIAN_POINT('Ctrl Pts',(21.2939982462078,-18.9549965668354,
8.63338091241178));
#146534=CARTESIAN_POINT('Ctrl Pts',(21.2938952958136,-19.0429481604934,
8.63776737442432));
#146535=CARTESIAN_POINT('Ctrl Pts',(21.2892548426303,-19.1307583016182,
8.64215383643686));
#146536=CARTESIAN_POINT('Ctrl Pts',(21.2801502518719,-19.2179302444115,
8.6465402984494));
#146537=CARTESIAN_POINT('Ctrl Pts',(21.2712189219787,-19.303443300316,8.65084328584743));
#146538=CARTESIAN_POINT('Ctrl Pts',(21.2579577432873,-19.3886695757442,
8.65514627324547));
#146539=CARTESIAN_POINT('Ctrl Pts',(21.2403952844639,-19.4731359496497,
8.65944926064351));
#146540=CARTESIAN_POINT('Ctrl Pts',(21.2233438132473,-19.555144736568,8.66362705069559));
#146541=CARTESIAN_POINT('Ctrl Pts',(21.2022379883831,-19.6364367360942,
8.66780484074767));
#146542=CARTESIAN_POINT('Ctrl Pts',(21.1771565050491,-19.7165824297198,
8.67198263079975));
#146543=CARTESIAN_POINT('Ctrl Pts',(21.1520996601068,-19.7966493935124,
8.67615631686697));
#146544=CARTESIAN_POINT('Ctrl Pts',(21.1230750478627,-19.8755718507968,
8.68033000293419));
#146545=CARTESIAN_POINT('Ctrl Pts',(21.0902120830425,-19.9529318756661,
8.68450368900141));
#146546=CARTESIAN_POINT('Ctrl Pts',(21.0573715411633,-20.030239116519,8.68867452729403));
#146547=CARTESIAN_POINT('Ctrl Pts',(21.020698028392,-20.1059856204581,8.69284536558666));
#146548=CARTESIAN_POINT('Ctrl Pts',(20.9803698817383,-20.1797712956488,
8.69701620387929));
#146549=CARTESIAN_POINT('Ctrl Pts',(20.9400571536068,-20.253528760615,8.70118544754959));
#146550=CARTESIAN_POINT('Ctrl Pts',(20.8960927897238,-20.3253264840432,
8.70535469121989));
#146551=CARTESIAN_POINT('Ctrl Pts',(20.8487014677721,-20.3947881695532,
8.70952393489019));
#146552=CARTESIAN_POINT('Ctrl Pts',(20.801299148321,-20.4642659741502,8.71369414606367));
#146553=CARTESIAN_POINT('Ctrl Pts',(20.7504685369908,-20.5314062746653,
8.71786435723714));
#146554=CARTESIAN_POINT('Ctrl Pts',(20.6964775883006,-20.5958618297831,
8.72203456841062));
#146555=CARTESIAN_POINT('Ctrl Pts',(20.6424782982004,-20.6603273430554,
8.72620542386693));
#146556=CARTESIAN_POINT('Ctrl Pts',(20.5853180035682,-20.7221069405515,
8.73037627932324));
#146557=CARTESIAN_POINT('Ctrl Pts',(20.5253036567636,-20.7808879706711,
8.73454713477954));
#146558=CARTESIAN_POINT('Ctrl Pts',(20.465239521452,-20.8397177661257,8.73872145041956));
#146559=CARTESIAN_POINT('Ctrl Pts',(20.4023169479903,-20.8955437192182,
8.74289576605959));
#146560=CARTESIAN_POINT('Ctrl Pts',(20.3368776276693,-20.948092009582,8.74707008169962));
#146561=CARTESIAN_POINT('Ctrl Pts',(20.3225496097124,-20.9595975210122,
8.74798405313383));
#146562=CARTESIAN_POINT('Ctrl Pts',(20.308101057154,-20.9709460624804,8.74889802456805));
#146563=CARTESIAN_POINT('Ctrl Pts',(20.2935357468249,-20.9821350335323,
8.74981199600226));
#146564=CARTESIAN_POINT('Ctrl Pts',(20.290984793813,-20.9788230549133,7.94987222229573));
#146565=CARTESIAN_POINT('Ctrl Pts',(19.966954935699,-21.2283578947164,7.97013523654456));
#146566=CARTESIAN_POINT('Ctrl Pts',(18.7905372718575,-21.7718985897377,
8.03279018635388));
#146567=CARTESIAN_POINT('Ctrl Pts',(16.7471750902531,-21.0909114965219,
8.12726281551246));
#146568=CARTESIAN_POINT('Ctrl Pts',(16.1802303010149,-19.5894613347174,
8.20147243042223));
#146569=CARTESIAN_POINT('Ctrl Pts',(16.1744184492745,-18.9496462808249,
8.23329010977151));
#146570=CARTESIAN_POINT('',(16.1740010575059,-18.9543268925436,8.16670989022852));
#146571=CARTESIAN_POINT('Ctrl Pts',(20.2961055615625,-20.9854720348234,
7.8832969629626));
#146572=CARTESIAN_POINT('Ctrl Pts',(20.2876322375241,-20.9919974145329,
7.88383131339138));
#146573=CARTESIAN_POINT('Ctrl Pts',(19.6033699017491,-21.511539674794,7.92675759938063));
#146574=CARTESIAN_POINT('Ctrl Pts',(17.6781136533722,-21.788969486026,8.01207582093036));
#146575=CARTESIAN_POINT('Ctrl Pts',(16.2739022033865,-20.1719439048314,
8.1060124462569));
#146576=CARTESIAN_POINT('Ctrl Pts',(16.1718447244466,-19.1382186602577,
8.15755713602294));
#146577=CARTESIAN_POINT('Ctrl Pts',(16.1735502429248,-18.9543273023083,
8.16670989022852));
#146578=CARTESIAN_POINT('Ctrl Pts',(16.1740010575059,-18.9543268925436,
8.16670989022852));
#146579=CARTESIAN_POINT('Ctrl Pts',(16.173925195224,-18.8708647825268,8.17086478789788));
#146580=CARTESIAN_POINT('Ctrl Pts',(16.1779353066412,-18.7872780169979,
8.17501968556725));
#146581=CARTESIAN_POINT('Ctrl Pts',(16.1860403077383,-18.7040052286649,
8.17917458323661));
#146582=CARTESIAN_POINT('Ctrl Pts',(16.1940671586084,-18.621535375116,8.18328941845664));
#146583=CARTESIAN_POINT('Ctrl Pts',(16.2061102365111,-18.539373952273,8.18740425367668));
#146584=CARTESIAN_POINT('Ctrl Pts',(16.2221259449782,-18.4579466307084,
8.19151908889671));
#146585=CARTESIAN_POINT('Ctrl Pts',(16.238134689091,-18.3765547174256,8.1956321348003));
#146586=CARTESIAN_POINT('Ctrl Pts',(16.2581125446655,-18.2958967363639,
8.19974518070389));
#146587=CARTESIAN_POINT('Ctrl Pts',(16.2819644394348,-18.216390314281,8.20385822660748));
#146588=CARTESIAN_POINT('Ctrl Pts',(16.3058135810414,-18.136893069419,8.2079707977528));
#146589=CARTESIAN_POINT('Ctrl Pts',(16.3335357367832,-18.0585475732033,
8.21208336889813));
#146590=CARTESIAN_POINT('Ctrl Pts',(16.3649858005362,-17.9817568744182,
8.21619594004345));
#146591=CARTESIAN_POINT('Ctrl Pts',(16.3969970744395,-17.9035958852594,
8.2203818978976));
#146592=CARTESIAN_POINT('Ctrl Pts',(16.4328704281987,-17.8270462022341,
8.22456785575175));
#146593=CARTESIAN_POINT('Ctrl Pts',(16.4724022025116,-17.7525103575288,
8.2287538136059));
#146594=CARTESIAN_POINT('Ctrl Pts',(16.5112918107485,-17.6791852955861,
8.23287177349699));
#146595=CARTESIAN_POINT('Ctrl Pts',(16.553721559467,-17.6078095092637,8.23698973338808));
#146596=CARTESIAN_POINT('Ctrl Pts',(16.5994527799561,-17.5387384653211,
8.24110769327917));
#146597=CARTESIAN_POINT('Ctrl Pts',(16.6463167081173,-17.467956614176,8.24532765011484));
#146598=CARTESIAN_POINT('Ctrl Pts',(16.6966475137941,-17.3995956231065,
8.24954760695052));
#146599=CARTESIAN_POINT('Ctrl Pts',(16.7501447185243,-17.3340017854889,
8.25376756378619));
#146600=CARTESIAN_POINT('Ctrl Pts',(16.8036419232545,-17.2684079478714,
8.25798752062187));
#146601=CARTESIAN_POINT('Ctrl Pts',(16.8603051182412,-17.2055816046286,
8.26220747745754));
#146602=CARTESIAN_POINT('Ctrl Pts',(16.9197953580223,-17.1458268308308,
8.26642743429322));
#146603=CARTESIAN_POINT('Ctrl Pts',(16.9787876447051,-17.0865722243692,
8.27061206868627));
#146604=CARTESIAN_POINT('Ctrl Pts',(17.040795780927,-17.0301005497847,8.27479670307932));
#146605=CARTESIAN_POINT('Ctrl Pts',(17.1055265727615,-16.9767343731087,
8.27898133747237));
#146606=CARTESIAN_POINT('Ctrl Pts',(17.170165228326,-16.9234441565798,8.28316001555632));
#146607=CARTESIAN_POINT('Ctrl Pts',(17.2375184898922,-16.8732509480031,
8.28733869364027));
#146608=CARTESIAN_POINT('Ctrl Pts',(17.3072561423608,-16.8264407877716,
8.29151737172422));
#146609=CARTESIAN_POINT('Ctrl Pts',(17.3782437921302,-16.77879158906,8.29577094960966));
#146610=CARTESIAN_POINT('Ctrl Pts',(17.4517018138305,-16.7346482555831,
8.30002452749509));
#146611=CARTESIAN_POINT('Ctrl Pts',(17.5272463530815,-16.6942698045052,
8.30427810538053));
#146612=CARTESIAN_POINT('Ctrl Pts',(17.6013263140262,-16.6546741684935,
8.30844921935848));
#146613=CARTESIAN_POINT('Ctrl Pts',(17.6774121876528,-16.6186989652307,
8.31262033333643));
#146614=CARTESIAN_POINT('Ctrl Pts',(17.7551140500804,-16.5865439557984,
8.31679144731439));
#146615=CARTESIAN_POINT('Ctrl Pts',(17.8327898388978,-16.55439973629,8.32096116163476));
#146616=CARTESIAN_POINT('Ctrl Pts',(17.9120801148583,-16.5260733404923,
8.32513087595514));
#146617=CARTESIAN_POINT('Ctrl Pts',(17.9925737212266,-16.5017169401997,
8.32930059027551));
#146618=CARTESIAN_POINT('Ctrl Pts',(18.0730644632869,-16.4773614066124,
8.33347015621955));
#146619=CARTESIAN_POINT('Ctrl Pts',(18.1547580100548,-16.456975720069,8.3376397221636));
#146620=CARTESIAN_POINT('Ctrl Pts',(18.2372280581084,-16.440662181675,8.34180928810765));
#146621=CARTESIAN_POINT('Ctrl Pts',(18.3225976513137,-16.4237750793961,
8.34612545084656));
#146622=CARTESIAN_POINT('Ctrl Pts',(18.4087988479278,-16.4112519089493,
8.35044161358548));
#146623=CARTESIAN_POINT('Ctrl Pts',(18.4953492973486,-16.4031481325656,
8.3547577763244));
#146624=CARTESIAN_POINT('Ctrl Pts',(18.5790803749831,-16.3953083358451,
8.35893334051608));
#146625=CARTESIAN_POINT('Ctrl Pts',(18.6631378283663,-16.3916044048151,
8.36310890470776));
#146626=CARTESIAN_POINT('Ctrl Pts',(18.7470834485361,-16.392033433153,8.36728446889944));
#146627=CARTESIAN_POINT('Ctrl Pts',(18.8352689624189,-16.3924841306924,
8.37167093091198));
#146628=CARTESIAN_POINT('Ctrl Pts',(18.9233304658572,-16.3974962383813,
8.37605739292452));
#146629=CARTESIAN_POINT('Ctrl Pts',(19.0107666109438,-16.4070048638422,
8.38044385493706));
#146630=CARTESIAN_POINT('Ctrl Pts',(19.0982027560304,-16.4165134893032,
8.38483031694959));
#146631=CARTESIAN_POINT('Ctrl Pts',(19.1850129820695,-16.4305184650313,
8.38921677896213));
#146632=CARTESIAN_POINT('Ctrl Pts',(19.2707112385804,-16.4488937205181,
8.39360324097467));
#146633=CARTESIAN_POINT('Ctrl Pts',(19.3524663912739,-16.4664235032614,
8.39778787536771));
#146634=CARTESIAN_POINT('Ctrl Pts',(19.4335139608228,-16.4879954864411,
8.40197250976076));
#146635=CARTESIAN_POINT('Ctrl Pts',(19.5134240199301,-16.5135377392389,
8.40615714415381));
#146636=CARTESIAN_POINT('Ctrl Pts',(19.5932203369592,-16.5390436358014,
8.41033582223775));
#146637=CARTESIAN_POINT('Ctrl Pts',(19.6718819251547,-16.5685084380806,
8.41451450032169));
#146638=CARTESIAN_POINT('Ctrl Pts',(19.7489895306428,-16.6018093156755,
8.41869317840564));
#146639=CARTESIAN_POINT('Ctrl Pts',(19.827479234543,-16.6357070875684,8.42294675629107));
#146640=CARTESIAN_POINT('Ctrl Pts',(19.904358226068,-16.6735797096679,8.42720033417651));
#146641=CARTESIAN_POINT('Ctrl Pts',(19.9792009396772,-16.7152446222649,
8.43145391206194));
#146642=CARTESIAN_POINT('Ctrl Pts',(20.0525926812396,-16.7561017792288,
8.4356250260399));
#146643=CARTESIAN_POINT('Ctrl Pts',(20.1240259742956,-16.8006052628958,
8.43979614001785));
#146644=CARTESIAN_POINT('Ctrl Pts',(20.1931217929874,-16.8485353358734,
8.44396725399581));
#146645=CARTESIAN_POINT('Ctrl Pts',(20.2621944259099,-16.8964493254521,
8.44813696831618));
#146646=CARTESIAN_POINT('Ctrl Pts',(20.3289307645448,-16.9477873587841,
8.45230668263656));
#146647=CARTESIAN_POINT('Ctrl Pts',(20.3929803051522,-17.0022860858277,
8.45647639695693));
#146648=CARTESIAN_POINT('Ctrl Pts',(20.457027566602,-17.0567828735727,8.46064596290098));
#146649=CARTESIAN_POINT('Ctrl Pts',(20.518387870305,-17.1144398326397,8.46481552884503));
#146650=CARTESIAN_POINT('Ctrl Pts',(20.5767444472642,-17.1749538829628,
8.46898509478907));
#146651=CARTESIAN_POINT('Ctrl Pts',(20.6371527694786,-17.2375955326431,
8.47330125752799));
#146652=CARTESIAN_POINT('Ctrl Pts',(20.6943418467819,-17.3032985427184,
8.47761742026691));
#146653=CARTESIAN_POINT('Ctrl Pts',(20.7480039569826,-17.3716873533195,
8.48193358300583));
#146654=CARTESIAN_POINT('Ctrl Pts',(20.7999180295879,-17.4378484056085,
8.48610914719751));
#146655=CARTESIAN_POINT('Ctrl Pts',(20.848531154665,-17.5065225539075,8.4902847113892));
#146656=CARTESIAN_POINT('Ctrl Pts',(20.8936085817713,-17.5773397606901,
8.49446027558088));
#146657=CARTESIAN_POINT('Ctrl Pts',(20.9409627625594,-17.6517337762353,
8.49884673759342));
#146658=CARTESIAN_POINT('Ctrl Pts',(20.9844143947689,-17.7284925234218,
8.50323319960595));
#146659=CARTESIAN_POINT('Ctrl Pts',(21.0237466725066,-17.8071593229863,
8.50761966161849));
#146660=CARTESIAN_POINT('Ctrl Pts',(21.0630789502442,-17.8858261225508,
8.51200612363103));
#146661=CARTESIAN_POINT('Ctrl Pts',(21.0982917108611,-17.9664004123699,
8.51639258564357));
#146662=CARTESIAN_POINT('Ctrl Pts',(21.1292278697973,-18.0484052613331,
8.5207790476561));
#146663=CARTESIAN_POINT('Ctrl Pts',(21.1587406102024,-18.1266369456354,
8.52496368204915));
#146664=CARTESIAN_POINT('Ctrl Pts',(21.1844714983967,-18.2064616309202,
8.5291483164422));
#146665=CARTESIAN_POINT('Ctrl Pts',(21.2062483053235,-18.2874788815808,
8.53333295083525));
#146666=CARTESIAN_POINT('Ctrl Pts',(21.2279941156611,-18.3683808142131,
8.5375116289192));
#146667=CARTESIAN_POINT('Ctrl Pts',(21.2457969056056,-18.4504715000491,
8.54169030700315));
#146668=CARTESIAN_POINT('Ctrl Pts',(21.2595330219157,-18.5333319271626,
8.5458689850871));
#146669=CARTESIAN_POINT('Ctrl Pts',(21.2735153482387,-18.6176775678812,
8.55012256297253));
#146670=CARTESIAN_POINT('Ctrl Pts',(21.2832836065124,-18.7028203654208,
8.55437614085796));
#146671=CARTESIAN_POINT('Ctrl Pts',(21.2887609500061,-18.7883036704011,
8.5586297187434));
#146672=CARTESIAN_POINT('Ctrl Pts',(21.2941321045079,-18.8721297147074,
8.56280083272135));
#146673=CARTESIAN_POINT('Ctrl Pts',(21.2953772042646,-18.9562827012374,
8.5669719466993));
#146674=CARTESIAN_POINT('Ctrl Pts',(21.2924758541409,-19.0403249895437,
8.57114306067725));
#146675=CARTESIAN_POINT('Ctrl Pts',(21.2895754775933,-19.1243390766486,
8.57531277499763));
#146676=CARTESIAN_POINT('Ctrl Pts',(21.2825314303294,-19.2082420799258,
8.57948248931799));
#146677=CARTESIAN_POINT('Ctrl Pts',(21.2713754270314,-19.2915967348155,
8.58365220363837));
#146678=CARTESIAN_POINT('Ctrl Pts',(21.2602198207118,-19.3749484235889,
8.58782176958241));
#146679=CARTESIAN_POINT('Ctrl Pts',(21.2449526111524,-19.4577513469167,
8.59199133552645));
#146680=CARTESIAN_POINT('Ctrl Pts',(21.2256571796747,-19.5395751007108,
8.59616090147049));
#146681=CARTESIAN_POINT('Ctrl Pts',(21.2056833446298,-19.624275676748,8.60047706420941));
#146682=CARTESIAN_POINT('Ctrl Pts',(21.1813928737509,-19.7079264335899,
8.60479322694833));
#146683=CARTESIAN_POINT('Ctrl Pts',(21.1529349892686,-19.7900653421377,
8.60910938968725));
#146684=CARTESIAN_POINT('Ctrl Pts',(21.12540411738,-19.869528584379,8.61328495387892));
#146685=CARTESIAN_POINT('Ctrl Pts',(21.0939733891636,-19.9475765433409,
8.6174605180706));
#146686=CARTESIAN_POINT('Ctrl Pts',(21.0588268816571,-20.0238115367567,
8.62163608226228));
#146687=CARTESIAN_POINT('Ctrl Pts',(21.0219052076092,-20.1038969784584,
8.62602254427482));
#146688=CARTESIAN_POINT('Ctrl Pts',(20.9808827929501,-20.181980978784,8.63040900628737));
#146689=CARTESIAN_POINT('Ctrl Pts',(20.936026279751,-20.257634046464,8.63479546829991));
#146690=CARTESIAN_POINT('Ctrl Pts',(20.8911697665519,-20.333287114144,8.63918193031245));
#146691=CARTESIAN_POINT('Ctrl Pts',(20.842479539431,-20.4065088081494,8.64356839232499));
#146692=CARTESIAN_POINT('Ctrl Pts',(20.790271595083,-20.4769088914603,8.64795485433753));
#146693=CARTESIAN_POINT('Ctrl Pts',(20.7404694331031,-20.5440648845997,
8.6521391847952));
#146694=CARTESIAN_POINT('Ctrl Pts',(20.6872812569759,-20.6089035367256,
8.65632351525286));
#146695=CARTESIAN_POINT('Ctrl Pts',(20.6309504906871,-20.6710633600545,
8.66050784571053));
#146696=CARTESIAN_POINT('Ctrl Pts',(20.5747060923804,-20.7331278781203,
8.66468576063008));
#146697=CARTESIAN_POINT('Ctrl Pts',(20.5153289851622,-20.7925213917038,
8.66886367554964));
#146698=CARTESIAN_POINT('Ctrl Pts',(20.4531043975684,-20.8489133006706,
8.67304159046919));
#146699=CARTESIAN_POINT('Ctrl Pts',(20.4017904533731,-20.8954172853764,
8.67648693741844));
#146700=CARTESIAN_POINT('Ctrl Pts',(20.34854091394,-20.9398804430942,8.67993228436769));
#146701=CARTESIAN_POINT('Ctrl Pts',(20.2935357468249,-20.9821350335323,
8.68337763131693));
#146702=CARTESIAN_POINT('Origin',(18.734,-18.952,-1.76670989022851));
#146703=CARTESIAN_POINT('',(20.2954164701606,-20.9846205560609,9.5499633223245));
#146704=CARTESIAN_POINT('',(20.2935357468249,-20.9821350335323,9.48328065736197));
#146705=CARTESIAN_POINT('',(20.2935357468249,-20.9821350335323,-1.76670989022851));
#146706=CARTESIAN_POINT('',(16.1736699172806,-18.9526425113319,9.03329016588271));
#146707=CARTESIAN_POINT('Ctrl Pts',(16.1699656690245,-18.9526308403706,
9.03329079541859));
#146708=CARTESIAN_POINT('Ctrl Pts',(16.1727141322405,-18.1388729144851,
9.07394170533744));
#146709=CARTESIAN_POINT('Ctrl Pts',(17.0319371704071,-16.4715241260563,
9.15698455081677));
#146710=CARTESIAN_POINT('Ctrl Pts',(19.8732646791955,-16.1474739147344,
9.28241933185658));
#146711=CARTESIAN_POINT('Ctrl Pts',(21.7088249748179,-18.3919045247491,
9.40959513853799));
#146712=CARTESIAN_POINT('Ctrl Pts',(21.0821529663045,-20.3261355156988,
9.49877646869399));
#146713=CARTESIAN_POINT('Ctrl Pts',(20.3656977374887,-20.9314719539678,
9.54556586328949));
#146714=CARTESIAN_POINT('Ctrl Pts',(20.2954164701606,-20.9846205560609,
9.5499633223245));
#146715=CARTESIAN_POINT('Ctrl Pts',(20.2935357468249,-20.9821350335323,
8.74981199600226));
#146716=CARTESIAN_POINT('Ctrl Pts',(20.226866111391,-21.0333501881746,8.75399550743729));
#146717=CARTESIAN_POINT('Ctrl Pts',(20.1577482566508,-21.081218427346,8.75817901887232));
#146718=CARTESIAN_POINT('Ctrl Pts',(20.0865601504742,-21.1255181249185,
8.76236253030735));
#146719=CARTESIAN_POINT('Ctrl Pts',(20.0221613392068,-21.1655929072999,
8.76614705524851));
#146720=CARTESIAN_POINT('Ctrl Pts',(19.9560688974245,-21.2027478334321,
8.76993158018967));
#146721=CARTESIAN_POINT('Ctrl Pts',(19.8885775886028,-21.2368524223451,
8.77371610513083));
#146722=CARTESIAN_POINT('Ctrl Pts',(19.8139509296381,-21.2745626337838,
8.77790073952388));
#146723=CARTESIAN_POINT('Ctrl Pts',(19.7373359438749,-21.3086830520783,
8.78208537391693));
#146724=CARTESIAN_POINT('Ctrl Pts',(19.6591123506694,-21.3389996101045,
8.78627000830997));
#146725=CARTESIAN_POINT('Ctrl Pts',(19.5810000990667,-21.3692730162627,
8.79044868639392));
#146726=CARTESIAN_POINT('Ctrl Pts',(19.5012842132702,-21.3957531518832,
8.79462736447786));
#146727=CARTESIAN_POINT('Ctrl Pts',(19.4203680775091,-21.4182722603509,
8.79880604256181));
#146728=CARTESIAN_POINT('Ctrl Pts',(19.3380015781678,-21.4411950076538,
8.80305962044724));
#146729=CARTESIAN_POINT('Ctrl Pts',(19.2543918069889,-21.4600131107993,
8.80731319833268));
#146730=CARTESIAN_POINT('Ctrl Pts',(19.1699845756622,-21.4746013259698,
8.81156677621811));
#146731=CARTESIAN_POINT('Ctrl Pts',(19.0872137432219,-21.4889067201227,
8.81573789019606));
#146732=CARTESIAN_POINT('Ctrl Pts',(19.0036765695344,-21.4991446900207,
8.81990900417402));
#146733=CARTESIAN_POINT('Ctrl Pts',(18.9198060037776,-21.5052481526401,
8.82408011815197));
#146734=CARTESIAN_POINT('Ctrl Pts',(18.8359635815991,-21.5113495671838,
8.82824983247234));
#146735=CARTESIAN_POINT('Ctrl Pts',(18.7517884479705,-21.5133191964338,
8.83241954679272));
#146736=CARTESIAN_POINT('Ctrl Pts',(18.6677187513895,-21.5111418085137,
8.83658926111309));
#146737=CARTESIAN_POINT('Ctrl Pts',(18.5836520463691,-21.5089644980744,
8.84075882705713));
#146738=CARTESIAN_POINT('Ctrl Pts',(18.4996912307932,-21.502640476632,8.84492839300118));
#146739=CARTESIAN_POINT('Ctrl Pts',(18.4162731576902,-21.4922066163357,
8.84909795894522));
#146740=CARTESIAN_POINT('Ctrl Pts',(18.3299222080443,-21.481405914383,8.85341412168414));
#146741=CARTESIAN_POINT('Ctrl Pts',(18.2441533999762,-21.4662010579768,
8.85773028442306));
#146742=CARTESIAN_POINT('Ctrl Pts',(18.1594420717104,-21.4466910003124,
8.86204644716198));
#146743=CARTESIAN_POINT('Ctrl Pts',(18.0774902060527,-21.4278164807242,
8.86622201135366));
#146744=CARTESIAN_POINT('Ctrl Pts',(17.996528423794,-21.404913110059,8.87039757554534));
#146745=CARTESIAN_POINT('Ctrl Pts',(17.9169718130409,-21.3781213781908,
8.87457313973702));
#146746=CARTESIAN_POINT('Ctrl Pts',(17.8333969870066,-21.3499764596372,
8.87895960174956));
#146747=CARTESIAN_POINT('Ctrl Pts',(17.7513735563979,-21.3175402693169,
8.88334606376211));
#146748=CARTESIAN_POINT('Ctrl Pts',(17.6713570660693,-21.2810319866776,
8.88773252577465));
#146749=CARTESIAN_POINT('Ctrl Pts',(17.5913405757408,-21.2445237040383,
8.89211898778719));
#146750=CARTESIAN_POINT('Ctrl Pts',(17.513331505326,-21.203943664325,8.89650544979973));
#146751=CARTESIAN_POINT('Ctrl Pts',(17.4377516489576,-21.159564316712,8.90089191181227));
#146752=CARTESIAN_POINT('Ctrl Pts',(17.3656493338169,-21.1172269286685,
8.90507654620532));
#146753=CARTESIAN_POINT('Ctrl Pts',(17.295489223029,-21.0712745855039,8.90926118059836));
#146754=CARTESIAN_POINT('Ctrl Pts',(17.227656848054,-21.0219107006307,8.91344581499141));
#146755=CARTESIAN_POINT('Ctrl Pts',(17.1599210240689,-20.9726170791376,
8.91762449307535));
#146756=CARTESIAN_POINT('Ctrl Pts',(17.0945067235341,-20.919921829671,8.9218031711593));
#146757=CARTESIAN_POINT('Ctrl Pts',(17.0317733474473,-20.8640733310569,
8.92598184924324));
#146758=CARTESIAN_POINT('Ctrl Pts',(16.9679155206798,-20.8072237882428,
8.93023542712867));
#146759=CARTESIAN_POINT('Ctrl Pts',(16.9068360906094,-20.7471070845336,
8.93448900501411));
#146760=CARTESIAN_POINT('Ctrl Pts',(16.8488816768787,-20.6840302849062,
8.93874258289955));
#146761=CARTESIAN_POINT('Ctrl Pts',(16.7920508225469,-20.6221763521239,
8.9429136968775));
#146762=CARTESIAN_POINT('Ctrl Pts',(16.7382252223473,-20.5574764280243,
8.94708481085545));
#146763=CARTESIAN_POINT('Ctrl Pts',(16.6876956296652,-20.4902582435822,
8.9512559248334));
#146764=CARTESIAN_POINT('Ctrl Pts',(16.6371829926759,-20.423062614851,8.95542563915378));
#146765=CARTESIAN_POINT('Ctrl Pts',(16.5899644428517,-20.3533507714291,
8.95959535347415));
#146766=CARTESIAN_POINT('Ctrl Pts',(16.546289949262,-20.2814828821387,8.96376506779452));
#146767=CARTESIAN_POINT('Ctrl Pts',(16.5026170097982,-20.2096175502162,
8.96793463373857));
#146768=CARTESIAN_POINT('Ctrl Pts',(16.4624881140047,-20.1355967185418,
8.97210419968261));
#146769=CARTESIAN_POINT('Ctrl Pts',(16.426108718498,-20.0598076695739,8.97627376562665));
#146770=CARTESIAN_POINT('Ctrl Pts',(16.388450268324,-19.9813539711403,8.98058992836557));
#146771=CARTESIAN_POINT('Ctrl Pts',(16.3548101172678,-19.9010058763734,
8.98490609110449));
#146772=CARTESIAN_POINT('Ctrl Pts',(16.3253623529171,-19.8192166309839,
8.98922225384341));
#146773=CARTESIAN_POINT('Ctrl Pts',(16.2968738463928,-19.7400916616603,
8.99339781803509));
#146774=CARTESIAN_POINT('Ctrl Pts',(16.2723088794103,-19.6596184551162,
8.99757338222677));
#146775=CARTESIAN_POINT('Ctrl Pts',(16.2517740015378,-19.5782220792646,
9.00174894641845));
#146776=CARTESIAN_POINT('Ctrl Pts',(16.230201955801,-19.4927145659702,9.00613540843099));
#146777=CARTESIAN_POINT('Ctrl Pts',(16.213077931431,-19.4061887466983,9.01052187044353));
#146778=CARTESIAN_POINT('Ctrl Pts',(16.2004642109875,-19.3191463002578,
9.01490833245608));
#146779=CARTESIAN_POINT('Ctrl Pts',(16.1878504905441,-19.2321038538173,
9.01929479446862));
#146780=CARTESIAN_POINT('Ctrl Pts',(16.179747051756,-19.144545364966,9.02368125648116));
#146781=CARTESIAN_POINT('Ctrl Pts',(16.1761531171477,-19.0569729673897,
9.0280677184937));
#146782=CARTESIAN_POINT('Ctrl Pts',(16.1747268399112,-19.022219269613,9.0298085155863));
#146783=CARTESIAN_POINT('Ctrl Pts',(16.1740088273484,-18.9874363059254,
9.0315493126789));
#146784=CARTESIAN_POINT('Ctrl Pts',(16.1740000808904,-18.9526435515772,
9.0332901097715));
#146785=CARTESIAN_POINT('',(16.174000001606,-18.9519093211995,8.96670989026365));
#146786=CARTESIAN_POINT('Ctrl Pts',(20.2935357468249,-20.9821350335323,
8.68337763131693));
#146787=CARTESIAN_POINT('Ctrl Pts',(20.2269370171092,-21.0332957188903,
8.68754916178006));
#146788=CARTESIAN_POINT('Ctrl Pts',(20.1577639337492,-21.0812174419311,
8.69172069224319));
#146789=CARTESIAN_POINT('Ctrl Pts',(20.0863674114257,-21.1256380527848,
8.69589222270632));
#146790=CARTESIAN_POINT('Ctrl Pts',(20.0149990010201,-21.1700411733108,
8.70006211065636));
#146791=CARTESIAN_POINT('Ctrl Pts',(19.941409280332,-21.2109456764381,8.7042319986064));
#146792=CARTESIAN_POINT('Ctrl Pts',(19.865978108956,-21.2481327402492,8.70840188655645));
#146793=CARTESIAN_POINT('Ctrl Pts',(19.7905540105462,-21.2853163171353,
8.71257138350797));
#146794=CARTESIAN_POINT('Ctrl Pts',(19.7132892174036,-21.3187829444825,
8.71674088045949));
#146795=CARTESIAN_POINT('Ctrl Pts',(19.6345869215609,-21.3483604062648,
8.72091037741101));
#146796=CARTESIAN_POINT('Ctrl Pts',(19.5558683969919,-21.3779439670372,
8.72508073412939));
#146797=CARTESIAN_POINT('Ctrl Pts',(19.4757122121442,-21.4036366092316,
8.72925109084776));
#146798=CARTESIAN_POINT('Ctrl Pts',(19.3945389058334,-21.42531525566,8.73342144756614));
#146799=CARTESIAN_POINT('Ctrl Pts',(19.3132745301638,-21.4470182236359,
8.73759648306045));
#146800=CARTESIAN_POINT('Ctrl Pts',(19.230991201076,-21.464698091023,8.74177151855476));
#146801=CARTESIAN_POINT('Ctrl Pts',(19.1481213446228,-21.4782825479205,
8.74594655404907));
#146802=CARTESIAN_POINT('Ctrl Pts',(19.0651969871444,-21.4918759389089,
8.75012433533931));
#146803=CARTESIAN_POINT('Ctrl Pts',(18.9816857911789,-21.5013685073529,
8.75430211662955));
#146804=CARTESIAN_POINT('Ctrl Pts',(18.8980246552272,-21.5067398913544,
8.75847989791979));
#146805=CARTESIAN_POINT('Ctrl Pts',(18.8142288831572,-21.5121199195404,
8.76266440252606));
#146806=CARTESIAN_POINT('Ctrl Pts',(18.730283148478,-21.5133655227373,8.76684890713234));
#146807=CARTESIAN_POINT('Ctrl Pts',(18.6466231642283,-21.5105084108852,
8.77103341173861));
#146808=CARTESIAN_POINT('Ctrl Pts',(18.6193179957145,-21.5095758991081,
8.77239916149873));
#146809=CARTESIAN_POINT('Ctrl Pts',(18.5920432114748,-21.5082067533533,
8.77376491125885));
#146810=CARTESIAN_POINT('Ctrl Pts',(18.5648137584889,-21.5064032601928,
8.77513066101898));
#146811=CARTESIAN_POINT('Ctrl Pts',(18.481383170547,-21.5008773873516,8.77931529541203));
#146812=CARTESIAN_POINT('Ctrl Pts',(18.3980683312292,-21.4912494832413,
8.78349992980508));
#146813=CARTESIAN_POINT('Ctrl Pts',(18.3153050503464,-21.4775285662876,
8.78768456419813));
#146814=CARTESIAN_POINT('Ctrl Pts',(18.2326595727498,-21.4638271793608,
8.79186324228208));
#146815=CARTESIAN_POINT('Ctrl Pts',(18.1505645441386,-21.4460444262516,
8.79604192036603));
#146816=CARTESIAN_POINT('Ctrl Pts',(18.0694525718369,-21.4242412333188,
8.80022059844998));
#146817=CARTESIAN_POINT('Ctrl Pts',(17.9868867257261,-21.4020472338225,
8.80447417633541));
#146818=CARTESIAN_POINT('Ctrl Pts',(17.905340006223,-21.3756872759157,8.80872775422084));
#146819=CARTESIAN_POINT('Ctrl Pts',(17.8252599013634,-21.3452804752327,
8.81298133210628));
#146820=CARTESIAN_POINT('Ctrl Pts',(17.7467323056,-21.3154631697149,8.81715244608422));
#146821=CARTESIAN_POINT('Ctrl Pts',(17.669615415452,-21.2817547038761,8.82132356006217));
#146822=CARTESIAN_POINT('Ctrl Pts',(17.5943160431832,-21.2443177089082,
8.82549467404012));
#146823=CARTESIAN_POINT('Ctrl Pts',(17.5190419383459,-21.2068932762856,
8.82966438836049));
#146824=CARTESIAN_POINT('Ctrl Pts',(17.4455845517327,-21.1657430039568,
8.83383410268086));
#146825=CARTESIAN_POINT('Ctrl Pts',(17.3743287784394,-21.1210768011437,
8.83800381700123));
#146826=CARTESIAN_POINT('Ctrl Pts',(17.3030755407324,-21.0764121877459,
8.84217338294526));
#146827=CARTESIAN_POINT('Ctrl Pts',(17.2340241499108,-21.0282321376739,
8.8463429488893));
#146828=CARTESIAN_POINT('Ctrl Pts',(17.1675318647118,-20.9767907499607,
8.85051251483333));
#146829=CARTESIAN_POINT('Ctrl Pts',(17.098701792792,-20.9235407465152,8.85482867757225));
#146830=CARTESIAN_POINT('Ctrl Pts',(17.0326145482173,-20.8667961238599,
8.85914484031117));
#146831=CARTESIAN_POINT('Ctrl Pts',(16.9696289167235,-20.8068840072893,
8.86346100305009));
#146832=CARTESIAN_POINT('Ctrl Pts',(16.9086950355507,-20.7489235216145,
8.86763656724177));
#146833=CARTESIAN_POINT('Ctrl Pts',(16.8506640912075,-20.6879991088315,
8.87181213143345));
#146834=CARTESIAN_POINT('Ctrl Pts',(16.7958218659397,-20.6244429797905,
8.87598769562512));
#146835=CARTESIAN_POINT('Ctrl Pts',(16.7382096902485,-20.5576767817618,
8.88037415763767));
#146836=CARTESIAN_POINT('Ctrl Pts',(16.6841171816934,-20.4880064858708,
8.88476061965022));
#146837=CARTESIAN_POINT('Ctrl Pts',(16.6338248927157,-20.4158526287654,
8.88914708166276));
#146838=CARTESIAN_POINT('Ctrl Pts',(16.583532603738,-20.34369877166,8.89353354367531));
#146839=CARTESIAN_POINT('Ctrl Pts',(16.537040776547,-20.2690618860433,8.89792000568785));
#146840=CARTESIAN_POINT('Ctrl Pts',(16.4945737975988,-20.192391181845,8.9023064677004));
#146841=CARTESIAN_POINT('Ctrl Pts',(16.4520961746315,-20.115701260729,8.90669402914565));
#146842=CARTESIAN_POINT('Ctrl Pts',(16.4134992022811,-20.0367143701648,
8.91108159059091));
#146843=CARTESIAN_POINT('Ctrl Pts',(16.3790251742675,-19.955839414531,8.91546915203616));
#146844=CARTESIAN_POINT('Ctrl Pts',(16.3446454932948,-19.8751857940064,
8.91984470579147));
#146845=CARTESIAN_POINT('Ctrl Pts',(16.3143664333075,-19.7926547636182,
8.92422025954678));
#146846=CARTESIAN_POINT('Ctrl Pts',(16.288384114166,-19.7086788876112,8.9285958133021));
#146847=CARTESIAN_POINT('Ctrl Pts',(16.262443998658,-19.624839415405,8.93296425975242));
#146848=CARTESIAN_POINT('Ctrl Pts',(16.2407868563188,-19.5395601416143,
8.93733270620274));
#146849=CARTESIAN_POINT('Ctrl Pts',(16.2235607960526,-19.4532933305799,
8.94170115265305));
#146850=CARTESIAN_POINT('Ctrl Pts',(16.2063704951608,-19.3672055997965,
8.94606053069714));
#146851=CARTESIAN_POINT('Ctrl Pts',(16.193593030381,-19.2801348014828,8.95041990874123));
#146852=CARTESIAN_POINT('Ctrl Pts',(16.1853263642748,-19.1925466660734,
8.95477928678532));
#146853=CARTESIAN_POINT('Ctrl Pts',(16.1777850503447,-19.1126438833577,
8.95875615459972));
#146854=CARTESIAN_POINT('Ctrl Pts',(16.1739971536887,-19.0323109723967,
8.96273302241411));
#146855=CARTESIAN_POINT('Ctrl Pts',(16.174000001606,-18.95190932191,8.96670989022851));
#146856=CARTESIAN_POINT('Ctrl Pts',(16.174000001606,-18.9519093211995,8.96670989026365));
#146857=CARTESIAN_POINT('Ctrl Pts',(16.1740031377284,-18.8633718327363,
8.97108917708311));
#146858=CARTESIAN_POINT('Ctrl Pts',(16.1786036643305,-18.7749281972307,
8.97546846390257));
#146859=CARTESIAN_POINT('Ctrl Pts',(16.1877467776185,-18.6870575014995,
8.97984775072203));
#146860=CARTESIAN_POINT('Ctrl Pts',(16.1969159526897,-18.5989363367042,
8.9842395203819));
#146861=CARTESIAN_POINT('Ctrl Pts',(16.2106535575188,-18.5113917635125,
8.98863129004177));
#146862=CARTESIAN_POINT('Ctrl Pts',(16.2288531973792,-18.4248951742598,
8.99302305970163));
#146863=CARTESIAN_POINT('Ctrl Pts',(16.2470794228643,-18.3382722327341,
8.99742124475989));
#146864=CARTESIAN_POINT('Ctrl Pts',(16.2697805833342,-18.2527007028955,
9.00181942981814));
#146865=CARTESIAN_POINT('Ctrl Pts',(16.2968004138022,-18.1686366251622,
9.00621761487639));
#146866=CARTESIAN_POINT('Ctrl Pts',(16.323895396912,-18.0843387325822,9.01062803299535));
#146867=CARTESIAN_POINT('Ctrl Pts',(16.3553329301084,-18.0015570394279,
9.0150384511143));
#146868=CARTESIAN_POINT('Ctrl Pts',(16.3909082116846,-17.9207285170583,
9.01944886923326));
#146869=CARTESIAN_POINT('Ctrl Pts',(16.4178853374885,-17.8594353629383,
9.02279333761612));
#146870=CARTESIAN_POINT('Ctrl Pts',(16.4472408225495,-17.7992649146788,
9.02613780599898));
#146871=CARTESIAN_POINT('Ctrl Pts',(16.4788683829461,-17.7403971815138,
9.02948227438184));
#146872=CARTESIAN_POINT('Ctrl Pts',(16.5184411227219,-17.6667412480013,
9.03366690877489));
#146873=CARTESIAN_POINT('Ctrl Pts',(16.5616998679758,-17.5948890389389,
9.03785154316794));
#146874=CARTESIAN_POINT('Ctrl Pts',(16.6084559713663,-17.5252335221418,
9.04203617756098));
#146875=CARTESIAN_POINT('Ctrl Pts',(16.6551455232309,-17.4556771513513,
9.04621485564493));
#146876=CARTESIAN_POINT('Ctrl Pts',(16.7053222910481,-17.3883116408714,
9.05039353372887));
#146877=CARTESIAN_POINT('Ctrl Pts',(16.7587517035101,-17.3235055519856,
9.05457221181281));
#146878=CARTESIAN_POINT('Ctrl Pts',(16.8131387997914,-17.2575378605319,
9.05882578969825));
#146879=CARTESIAN_POINT('Ctrl Pts',(16.8708960667841,-17.1942226731586,
9.06307936758369));
#146880=CARTESIAN_POINT('Ctrl Pts',(16.9317298045576,-17.1339180044288,
9.06733294546913));
#146881=CARTESIAN_POINT('Ctrl Pts',(16.9913841616171,-17.0747824593773,
9.07150405944708));
#146882=CARTESIAN_POINT('Ctrl Pts',(17.053996425417,-17.0185420838703,9.07567517342503));
#146883=CARTESIAN_POINT('Ctrl Pts',(17.1192501263854,-16.9654998500726,
9.07984628740298));
#146884=CARTESIAN_POINT('Ctrl Pts',(17.1844819308442,-16.9124754151088,
9.08401600172335));
#146885=CARTESIAN_POINT('Ctrl Pts',(17.2523530554691,-16.8626472804565,
9.08818571604372));
#146886=CARTESIAN_POINT('Ctrl Pts',(17.3225130695872,-16.8162788933773,
9.0923554303641));
#146887=CARTESIAN_POINT('Ctrl Pts',(17.3926705871108,-16.7699121562842,
9.09652499630814));
#146888=CARTESIAN_POINT('Ctrl Pts',(17.4651164479273,-16.7270051749183,
9.10069456225218));
#146889=CARTESIAN_POINT('Ctrl Pts',(17.5394714392695,-16.6877779442821,
9.10486412819623));
#146890=CARTESIAN_POINT('Ctrl Pts',(17.6164406603806,-16.6471715326088,
9.10918029093515));
#146891=CARTESIAN_POINT('Ctrl Pts',(17.6954552934392,-16.6105086923157,
9.11349645367407));
#146892=CARTESIAN_POINT('Ctrl Pts',(17.7760690203242,-16.5779805733361,
9.11781261641299));
#146893=CARTESIAN_POINT('Ctrl Pts',(17.854056763535,-16.546512054411,9.12198818060467));
#146894=CARTESIAN_POINT('Ctrl Pts',(17.9335405590282,-16.5189131263824,
9.12616374479635));
#146895=CARTESIAN_POINT('Ctrl Pts',(18.0140996850994,-16.4953063812095,
9.13033930898803));
#146896=CARTESIAN_POINT('Ctrl Pts',(18.0987276611173,-16.4705073154576,
9.13472577100057));
#146897=CARTESIAN_POINT('Ctrl Pts',(18.1845418843914,-16.4501144565313,
9.13911223301311));
#146898=CARTESIAN_POINT('Ctrl Pts',(18.2710433987721,-16.4342090663879,
9.14349869502565));
#146899=CARTESIAN_POINT('Ctrl Pts',(18.3575449131528,-16.4183036762444,
9.14788515703819));
#146900=CARTESIAN_POINT('Ctrl Pts',(18.4447331334585,-16.406885754803,9.15227161905074));
#146901=CARTESIAN_POINT('Ctrl Pts',(18.5321062576864,-16.3999735665917,
9.15665808106328));
#146902=CARTESIAN_POINT('Ctrl Pts',(18.6154592149507,-16.3933794184063,
9.16084271545632));
#146903=CARTESIAN_POINT('Ctrl Pts',(18.6992906902525,-16.3908609393394,
9.16502734984937));
#146904=CARTESIAN_POINT('Ctrl Pts',(18.7831681486199,-16.3924722128562,
9.16921198424242));
#146905=CARTESIAN_POINT('Ctrl Pts',(18.8669262178074,-16.3940811929245,
9.17339066232636));
#146906=CARTESIAN_POINT('Ctrl Pts',(18.9507296840397,-16.3998082408783,
9.17756934041031));
#146907=CARTESIAN_POINT('Ctrl Pts',(19.0341416766035,-16.4096556146018,
9.18174801849426));
#146908=CARTESIAN_POINT('Ctrl Pts',(19.1190487691868,-16.4196794954222,
9.1860015963797));
#146909=CARTESIAN_POINT('Ctrl Pts',(19.203549735092,-16.4339729066197,9.19025517426513));
#146910=CARTESIAN_POINT('Ctrl Pts',(19.2871845665267,-16.4524826795246,
9.19450875215056));
#146911=CARTESIAN_POINT('Ctrl Pts',(19.3691979735541,-16.4706336043628,
9.19867986612851));
#146912=CARTESIAN_POINT('Ctrl Pts',(19.4503780599826,-16.4928387610342,
9.20285098010647));
#146913=CARTESIAN_POINT('Ctrl Pts',(19.5302987751908,-16.5189960417974,
9.20702209408442));
#146914=CARTESIAN_POINT('Ctrl Pts',(19.6101926722311,-16.5451445452324,
9.21119180840479));
#146915=CARTESIAN_POINT('Ctrl Pts',(19.6888276004822,-16.5752423959817,
9.21536152272516));
#146916=CARTESIAN_POINT('Ctrl Pts',(19.7657923610116,-16.609137536312,9.21953123704553));
#146917=CARTESIAN_POINT('Ctrl Pts',(19.8427543828047,-16.6430314705078,
9.22370080298958));
#146918=CARTESIAN_POINT('Ctrl Pts',(19.9180459343719,-16.6807222394304,
9.22787036893362));
#146919=CARTESIAN_POINT('Ctrl Pts',(19.9912767740527,-16.7220100642766,
9.23203993487766));
#146920=CARTESIAN_POINT('Ctrl Pts',(20.0670823197167,-16.7647495181104,
9.23635609761658));
#146921=CARTESIAN_POINT('Ctrl Pts',(20.1406790886265,-16.8113434200911,
9.2406722603555));
#146922=CARTESIAN_POINT('Ctrl Pts',(20.2116647704045,-16.8615199531434,
9.24498842309442));
#146923=CARTESIAN_POINT('Ctrl Pts',(20.2803381010649,-16.9100619909092,
9.2491639872861));
#146924=CARTESIAN_POINT('Ctrl Pts',(20.3465675028829,-16.9619565080489,
9.25333955147778));
#146925=CARTESIAN_POINT('Ctrl Pts',(20.4100221667426,-17.0169161008919,
9.25751511566946));
#146926=CARTESIAN_POINT('Ctrl Pts',(20.4766817748247,-17.0746515721154,
9.26190157768201));
#146927=CARTESIAN_POINT('Ctrl Pts',(20.5402785534046,-17.135769485738,9.26628803969454));
#146928=CARTESIAN_POINT('Ctrl Pts',(20.6004740985359,-17.1998942841557,
9.27067450170708));
#146929=CARTESIAN_POINT('Ctrl Pts',(20.6606696436673,-17.2640190825733,
9.27506096371962));
#146930=CARTESIAN_POINT('Ctrl Pts',(20.7174636386703,-17.3311502736972,
9.27944742573216));
#146931=CARTESIAN_POINT('Ctrl Pts',(20.7705691100608,-17.4008758076974,
9.2838338877447));
#146932=CARTESIAN_POINT('Ctrl Pts',(20.8212311199914,-17.4673931665203,
9.28801852213775));
#146933=CARTESIAN_POINT('Ctrl Pts',(20.8687251499199,-17.5365189656785,
9.2922031565308));
#146934=CARTESIAN_POINT('Ctrl Pts',(20.9127716012343,-17.6079187860643,
9.29638779092385));
#146935=CARTESIAN_POINT('Ctrl Pts',(20.9567553578772,-17.6792169776434,
9.3005664690078));
#146936=CARTESIAN_POINT('Ctrl Pts',(20.9973010436862,-17.752782372994,9.30474514709174));
#146937=CARTESIAN_POINT('Ctrl Pts',(21.0341702903065,-17.8282488551324,
9.30892382517569));
#146938=CARTESIAN_POINT('Ctrl Pts',(21.0717003916751,-17.9050680197264,
9.31317740306112));
#146939=CARTESIAN_POINT('Ctrl Pts',(21.1054206649962,-17.9838567118702,
9.31743098094655));
#146940=CARTESIAN_POINT('Ctrl Pts',(21.1351268232139,-18.0641993586155,
9.32168455883199));
#146941=CARTESIAN_POINT('Ctrl Pts',(21.1642570695877,-18.1429844063779,
9.32585567280994));
#146942=CARTESIAN_POINT('Ctrl Pts',(21.1895272879509,-18.2232632421891,
9.33002678678789));
#146943=CARTESIAN_POINT('Ctrl Pts',(21.2107927216345,-18.3046223559169,
9.33419790076584));
#146944=CARTESIAN_POINT('Ctrl Pts',(21.2320510194963,-18.3859541688083,
9.33836761508622));
#146945=CARTESIAN_POINT('Ctrl Pts',(21.2493070853372,-18.46836509498,9.34253732940659));
#146946=CARTESIAN_POINT('Ctrl Pts',(21.2624662014641,-18.5514270752366,
9.34670704372697));
#146947=CARTESIAN_POINT('Ctrl Pts',(21.2756248493332,-18.6344860997914,
9.35087660967101));
#146948=CARTESIAN_POINT('Ctrl Pts',(21.284686766209,-18.7181956778688,9.35504617561505));
#146949=CARTESIAN_POINT('Ctrl Pts',(21.2896087040397,-18.8021195415125,
9.3592157415591));
#146950=CARTESIAN_POINT('Ctrl Pts',(21.2947036911327,-18.8889940646706,
9.36353190429802));
#146951=CARTESIAN_POINT('Ctrl Pts',(21.2953621283496,-18.9760976958014,
9.36784806703694));
#146952=CARTESIAN_POINT('Ctrl Pts',(21.2915948078576,-19.062945026117,9.37216422977586));
#146953=CARTESIAN_POINT('Ctrl Pts',(21.2879502074343,-19.1469633137823,
9.37633979396754));
#146954=CARTESIAN_POINT('Ctrl Pts',(21.2801638500693,-19.2307412775515,
9.38051535815922));
#146955=CARTESIAN_POINT('Ctrl Pts',(21.2682983360669,-19.3138451931541,
9.3846909223509));
#146956=CARTESIAN_POINT('Ctrl Pts',(21.2558335231597,-19.4011464899729,
9.38907738436344));
#146957=CARTESIAN_POINT('Ctrl Pts',(21.2388667599596,-19.4877032838011,
9.39346384637598));
#146958=CARTESIAN_POINT('Ctrl Pts',(21.2175306593405,-19.5730277482655,
9.39785030838852));
#146959=CARTESIAN_POINT('Ctrl Pts',(21.1961945587214,-19.65835221273,9.40223677040106));
#146960=CARTESIAN_POINT('Ctrl Pts',(21.1704893630394,-19.7424438151945,
9.4066232324136));
#146961=CARTESIAN_POINT('Ctrl Pts',(21.1406062076889,-19.8248382216158,
9.41100969442614));
#146962=CARTESIAN_POINT('Ctrl Pts',(21.1121004746695,-19.9034347728897,
9.41519396859539));
#146963=CARTESIAN_POINT('Ctrl Pts',(21.079687362158,-19.9807796693134,9.41937824276465));
#146964=CARTESIAN_POINT('Ctrl Pts',(21.0434966865728,-20.0564569048673,
9.4235625169339));
#146965=CARTESIAN_POINT('Ctrl Pts',(21.0073550560038,-20.13203158386,9.42774112064272));
#146966=CARTESIAN_POINT('Ctrl Pts',(20.9674462242502,-20.2059426782205,
9.43191972435153));
#146967=CARTESIAN_POINT('Ctrl Pts',(20.9239489993266,-20.2777916051735,
9.43609832806035));
#146968=CARTESIAN_POINT('Ctrl Pts',(20.8805019784913,-20.34955760477,9.44027210886403));
#146969=CARTESIAN_POINT('Ctrl Pts',(20.8334750334865,-20.419265776318,9.4444458896677));
#146970=CARTESIAN_POINT('Ctrl Pts',(20.7830933893995,-20.4865410654391,
9.44861967047138));
#146971=CARTESIAN_POINT('Ctrl Pts',(20.7327462827068,-20.5537702363118,
9.45279059008393));
#146972=CARTESIAN_POINT('Ctrl Pts',(20.679049319678,-20.6185694703057,9.45696150969649));
#146973=CARTESIAN_POINT('Ctrl Pts',(20.622270999894,-20.6805926735235,9.46113242930904));
#146974=CARTESIAN_POINT('Ctrl Pts',(20.5655043373564,-20.7426031426597,
9.46530249258352));
#146975=CARTESIAN_POINT('Ctrl Pts',(20.5056578783584,-20.801838367992,9.46947255585799));
#146976=CARTESIAN_POINT('Ctrl Pts',(20.4430396423786,-20.8579862278564,
9.47364261913246));
#146977=CARTESIAN_POINT('Ctrl Pts',(20.3947976124209,-20.9012433828251,
9.47685529854229));
#146978=CARTESIAN_POINT('Ctrl Pts',(20.3449112722043,-20.9426687088704,
9.48006797795213));
#146979=CARTESIAN_POINT('Ctrl Pts',(20.2935357468249,-20.9821350335323,
9.48328065736197));
#146980=CARTESIAN_POINT('Origin',(18.734,-18.952,-1.76670989022851));
#146981=CARTESIAN_POINT('',(20.2935357468249,-20.9821350335323,10.3499274775013));
#146982=CARTESIAN_POINT('',(20.2935357468249,-20.9821350335323,10.2832382198804));
#146983=CARTESIAN_POINT('',(20.2935357468249,-20.9821350335323,-1.76670989022851));
#146984=CARTESIAN_POINT('',(16.1740007840082,-18.9540035272626,9.83329010977151));
#146985=CARTESIAN_POINT('Ctrl Pts',(16.1740007840082,-18.9540035272626,
9.83329010977151));
#146986=CARTESIAN_POINT('Ctrl Pts',(16.1739350379054,-18.8699966984849,
9.83745593779553));
#146987=CARTESIAN_POINT('Ctrl Pts',(16.1780086491546,-18.7859395799201,
9.84162176581955));
#146988=CARTESIAN_POINT('Ctrl Pts',(16.186209790272,-18.7022700514274,9.84578759384357));
#146989=CARTESIAN_POINT('Ctrl Pts',(16.1944094741073,-18.6186153903909,
9.84995268163077));
#146990=CARTESIAN_POINT('Ctrl Pts',(16.2067351859308,-18.5353486407625,
9.85411776941798));
#146991=CARTESIAN_POINT('Ctrl Pts',(16.2231231591269,-18.4529033260309,
9.85828285720518));
#146992=CARTESIAN_POINT('Ctrl Pts',(16.2395131466374,-18.3704478776005,
9.86244845694076));
#146993=CARTESIAN_POINT('Ctrl Pts',(16.2599662961797,-18.2888145159801,
9.86661405667633));
#146994=CARTESIAN_POINT('Ctrl Pts',(16.284367851052,-18.2084259721855,9.87077965641191));
#146995=CARTESIAN_POINT('Ctrl Pts',(16.308796991805,-18.127946549396,9.87494996534484));
#146996=CARTESIAN_POINT('Ctrl Pts',(16.3371833166001,-18.0487151959129,
9.87912027427777));
#146997=CARTESIAN_POINT('Ctrl Pts',(16.3693624790262,-17.971138442795,9.8832905832107));
#146998=CARTESIAN_POINT('Ctrl Pts',(16.4015603628991,-17.8935165564619,
9.88746331837885));
#146999=CARTESIAN_POINT('Ctrl Pts',(16.4375552801455,-17.8175516031283,
9.89163605354699));
#147000=CARTESIAN_POINT('Ctrl Pts',(16.4771361744291,-17.7436268486807,
9.89580878871514));
#147001=CARTESIAN_POINT('Ctrl Pts',(16.5167895617088,-17.6695666999467,
9.89998916630976));
#147002=CARTESIAN_POINT('Ctrl Pts',(16.5600418069661,-17.5975546086437,
9.90416954390437));
#147003=CARTESIAN_POINT('Ctrl Pts',(16.606637749578,-17.5279459787355,9.90834992149899));
#147004=CARTESIAN_POINT('Ctrl Pts',(16.6436006876738,-17.4727278774588,
9.91166606942058));
#147005=CARTESIAN_POINT('Ctrl Pts',(16.6826668124626,-17.4190216712155,
9.91498221734216));
#147006=CARTESIAN_POINT('Ctrl Pts',(16.7236914224215,-17.3669891410737,
9.91829836526375));
#147007=CARTESIAN_POINT('Ctrl Pts',(16.7754602209958,-17.3013294900759,
9.9224829996568));
#147008=CARTESIAN_POINT('Ctrl Pts',(16.8305455538228,-17.2380865845811,
9.92666763404985));
#147009=CARTESIAN_POINT('Ctrl Pts',(16.8886933634202,-17.1776146368405,
9.93085226844289));
#147010=CARTESIAN_POINT('Ctrl Pts',(16.9467584068079,-17.1172287634326,
9.93503094652683));
#147011=CARTESIAN_POINT('Ctrl Pts',(17.0078769523775,-17.0596063422905,
9.93920962461078));
#147012=CARTESIAN_POINT('Ctrl Pts',(17.0717539579497,-17.0050695709173,
9.94338830269472));
#147013=CARTESIAN_POINT('Ctrl Pts',(17.1367759129393,-16.949555267112,9.94764188058016));
#147014=CARTESIAN_POINT('Ctrl Pts',(17.2046558928939,-16.897238700291,9.95189545846559));
#147015=CARTESIAN_POINT('Ctrl Pts',(17.2750424589416,-16.8484214078412,
9.95614903635103));
#147016=CARTESIAN_POINT('Ctrl Pts',(17.3440644440583,-16.8005505338647,
9.96032015032898));
#147017=CARTESIAN_POINT('Ctrl Pts',(17.415496297028,-16.7560447387742,9.96449126430694));
#147018=CARTESIAN_POINT('Ctrl Pts',(17.4889737195062,-16.7151473984905,
9.96866237828489));
#147019=CARTESIAN_POINT('Ctrl Pts',(17.5624264859257,-16.6742637817044,
9.97283209260527));
#147020=CARTESIAN_POINT('Ctrl Pts',(17.6379230570027,-16.6369864384995,
9.97700180692564));
#147021=CARTESIAN_POINT('Ctrl Pts',(17.7150725574696,-16.6035139202332,
9.98117152124602));
#147022=CARTESIAN_POINT('Ctrl Pts',(17.792219312626,-16.5700425930628,9.98534108719005));
#147023=CARTESIAN_POINT('Ctrl Pts',(17.8710184578634,-16.5403760039566,
9.98951065313409));
#147024=CARTESIAN_POINT('Ctrl Pts',(17.9510583236138,-16.5146649119628,
9.99368021907812));
#147025=CARTESIAN_POINT('Ctrl Pts',(18.0339122923043,-16.4880498496924,
9.99799638181705));
#147026=CARTESIAN_POINT('Ctrl Pts',(18.1180953501443,-16.4656737716517,
10.002312544556));
#147027=CARTESIAN_POINT('Ctrl Pts',(18.2031347548808,-16.4476473707713,
10.0066287072949));
#147028=CARTESIAN_POINT('Ctrl Pts',(18.2854040099525,-16.4302081780036,
10.0108042714866));
#147029=CARTESIAN_POINT('Ctrl Pts',(18.3684742051319,-16.4168396609885,
10.0149798356782));
#147030=CARTESIAN_POINT('Ctrl Pts',(18.4519097174443,-16.4075894449819,
10.0191553998699));
#147031=CARTESIAN_POINT('Ctrl Pts',(18.5395593591347,-16.3978720225551,
10.0235418618825));
#147032=CARTESIAN_POINT('Ctrl Pts',(18.6276116092808,-16.3926998996316,
10.027928323895));
#147033=CARTESIAN_POINT('Ctrl Pts',(18.7155609817196,-16.3920664066025,
10.0323147859076));
#147034=CARTESIAN_POINT('Ctrl Pts',(18.8035103541583,-16.3914329135735,
10.0367012479201));
#147035=CARTESIAN_POINT('Ctrl Pts',(18.8913562726231,-16.395337948682,10.0410877099327));
#147036=CARTESIAN_POINT('Ctrl Pts',(18.9786013944251,-16.403712308658,10.0454741719452));
#147037=CARTESIAN_POINT('Ctrl Pts',(19.0618322388445,-16.4117013519176,
10.0496588063382));
#147038=CARTESIAN_POINT('Ctrl Pts',(19.1448261598422,-16.4237872141345,
10.0538434407313));
#147039=CARTESIAN_POINT('Ctrl Pts',(19.2271478044735,-16.4399480015448,
10.0580280751243));
#147040=CARTESIAN_POINT('Ctrl Pts',(19.3093522744331,-16.4560857860745,
10.0622067532083));
#147041=CARTESIAN_POINT('Ctrl Pts',(19.3908859211795,-16.4762868870104,
10.0663854312922));
#147042=CARTESIAN_POINT('Ctrl Pts',(19.4713181268663,-16.5004776199687,
10.0705641093762));
#147043=CARTESIAN_POINT('Ctrl Pts',(19.5531920220344,-16.5251019544297,
10.0748176872616));
#147044=CARTESIAN_POINT('Ctrl Pts',(19.6339241211585,-16.5538603099738,
10.079071265147));
#147045=CARTESIAN_POINT('Ctrl Pts',(19.7130706518195,-16.5866203985944,
10.0833248430325));
#147046=CARTESIAN_POINT('Ctrl Pts',(19.7906827725418,-16.6187453689711,
10.0874959570104));
#147047=CARTESIAN_POINT('Ctrl Pts',(19.8667698102185,-16.6547181102194,
10.0916670709884));
#147048=CARTESIAN_POINT('Ctrl Pts',(19.9409299364305,-16.6943640398532,
10.0958381849663));
#147049=CARTESIAN_POINT('Ctrl Pts',(20.0150651774959,-16.7339966659124,
10.1000078992867));
#147050=CARTESIAN_POINT('Ctrl Pts',(20.0872743858819,-16.7772998157407,
10.1041776136071));
#147051=CARTESIAN_POINT('Ctrl Pts',(20.1571790379496,-16.8240522971791,
10.1083473279274));
#147052=CARTESIAN_POINT('Ctrl Pts',(20.22708120251,-16.8708031149636,10.1125168938715));
#147053=CARTESIAN_POINT('Ctrl Pts',(20.2946785918819,-16.9210027638615,
10.1166864598155));
#147054=CARTESIAN_POINT('Ctrl Pts',(20.3596216126349,-16.9743866979275,
10.1208560257596));
#147055=CARTESIAN_POINT('Ctrl Pts',(20.4268479498818,-17.029647545259,10.1251721884985));
#147056=CARTESIAN_POINT('Ctrl Pts',(20.4912293829736,-17.0883204279971,
10.1294883512374));
#147057=CARTESIAN_POINT('Ctrl Pts',(20.5524169502582,-17.1500677607041,
10.1338045139763));
#147058=CARTESIAN_POINT('Ctrl Pts',(20.6116113389742,-17.2098036805429,
10.137980078168));
#147059=CARTESIAN_POINT('Ctrl Pts',(20.66781646727,-17.2724164438391,10.1421556423597));
#147060=CARTESIAN_POINT('Ctrl Pts',(20.7207564953883,-17.3375655392576,
10.1463312065514));
#147061=CARTESIAN_POINT('Ctrl Pts',(20.7763703984738,-17.4060051606085,
10.1507176685639));
#147062=CARTESIAN_POINT('Ctrl Pts',(20.8283803483073,-17.4772435963692,
10.1551041305764));
#147063=CARTESIAN_POINT('Ctrl Pts',(20.8765183429015,-17.5508522025388,
10.159490592589));
#147064=CARTESIAN_POINT('Ctrl Pts',(20.9246563374958,-17.6244608087083,
10.1638770546015));
#147065=CARTESIAN_POINT('Ctrl Pts',(20.9689221504901,-17.7004390456585,
10.1682635166141));
#147066=CARTESIAN_POINT('Ctrl Pts',(21.0091047687182,-17.7783312684767,
10.1726499786266));
#147067=CARTESIAN_POINT('Ctrl Pts',(21.0474385251168,-17.8526395546591,
10.1768346130197));
#147068=CARTESIAN_POINT('Ctrl Pts',(21.0821992629535,-17.9289661561369,
10.1810192474127));
#147069=CARTESIAN_POINT('Ctrl Pts',(21.1131697431269,-18.0069331593007,
10.1852038818058));
#147070=CARTESIAN_POINT('Ctrl Pts',(21.1440961406553,-18.0847891860861,
10.1893825598897));
#147071=CARTESIAN_POINT('Ctrl Pts',(21.1712428282378,-18.1642805528131,
10.1935612379737));
#147072=CARTESIAN_POINT('Ctrl Pts',(21.1944386775071,-18.2450052940602,
10.1977399160576));
#147073=CARTESIAN_POINT('Ctrl Pts',(21.2180502957041,-18.327176968278,10.2019934939431));
#147074=CARTESIAN_POINT('Ctrl Pts',(21.2375678238505,-18.4106262399203,
10.2062470718285));
#147075=CARTESIAN_POINT('Ctrl Pts',(21.252862289631,-18.4949083616223,10.2105006497139));
#147076=CARTESIAN_POINT('Ctrl Pts',(21.2678602423477,-18.5775565099321,
10.2146717636919));
#147077=CARTESIAN_POINT('Ctrl Pts',(21.2787973301571,-18.6610050301441,
10.2188428776698));
#147078=CARTESIAN_POINT('Ctrl Pts',(21.2856028472,-18.7448215499602,10.2230139916478));
#147079=CARTESIAN_POINT('Ctrl Pts',(21.2924060805859,-18.8286099443337,
10.2271837059682));
#147080=CARTESIAN_POINT('Ctrl Pts',(21.2950804593957,-18.9127656349242,
10.2313534202885));
#147081=CARTESIAN_POINT('Ctrl Pts',(21.2936070835643,-18.9968506161339,
10.2355231346089));
#147082=CARTESIAN_POINT('Ctrl Pts',(21.2921337601619,-19.0809326052393,
10.239692700553));
#147083=CARTESIAN_POINT('Ctrl Pts',(21.2865129844866,-19.1649434300193,
10.243862266497));
#147084=CARTESIAN_POINT('Ctrl Pts',(21.2767779695195,-19.2484459440205,
10.2480318324411));
#147085=CARTESIAN_POINT('Ctrl Pts',(21.2667006834357,-19.3348843034021,
10.25234799518));
#147086=CARTESIAN_POINT('Ctrl Pts',(21.2522145228801,-19.4207774186565,
10.2566641579189));
#147087=CARTESIAN_POINT('Ctrl Pts',(21.2334144574579,-19.5056491396638,
10.2609803206578));
#147088=CARTESIAN_POINT('Ctrl Pts',(21.2152268021894,-19.5877561732863,
10.2651558848495));
#147089=CARTESIAN_POINT('Ctrl Pts',(21.1930021468738,-19.6689068927559,
10.2693314490412));
#147090=CARTESIAN_POINT('Ctrl Pts',(21.166877500828,-19.748685048162,10.2735070132329));
#147091=CARTESIAN_POINT('Ctrl Pts',(21.1394333610159,-19.8324926085429,
10.2778934752454));
#147092=CARTESIAN_POINT('Ctrl Pts',(21.1076851096662,-19.9147847597333,
10.2822799372579));
#147093=CARTESIAN_POINT('Ctrl Pts',(21.0718481041567,-19.995104137606,10.2866663992705));
#147094=CARTESIAN_POINT('Ctrl Pts',(21.0360110986473,-20.0754235154787,
10.291052861283));
#147095=CARTESIAN_POINT('Ctrl Pts',(20.9960856701951,-20.15376963761,10.2954393232955));
#147096=CARTESIAN_POINT('Ctrl Pts',(20.9523407266399,-20.2297184433712,
10.2998257853081));
#147097=CARTESIAN_POINT('Ctrl Pts',(20.9106208944249,-20.3021513047666,
10.3040091821606));
#147098=CARTESIAN_POINT('Ctrl Pts',(20.8652721209666,-20.3726734304945,
10.308192579013));
#147099=CARTESIAN_POINT('Ctrl Pts',(20.8164943998492,-20.4408979396173,
10.3123759758655));
#147100=CARTESIAN_POINT('Ctrl Pts',(20.7677772522441,-20.509037725673,10.316554177661));
#147101=CARTESIAN_POINT('Ctrl Pts',(20.7156398718315,-20.5748851865346,
10.3207323794565));
#147102=CARTESIAN_POINT('Ctrl Pts',(20.6603275198092,-20.6380789680278,
10.324910581252));
#147103=CARTESIAN_POINT('Ctrl Pts',(20.6050732438228,-20.7012063982598,
10.3290843960816));
#147104=CARTESIAN_POINT('Ctrl Pts',(20.5466509193235,-20.7616853395333,
10.3332582109113));
#147105=CARTESIAN_POINT('Ctrl Pts',(20.4853475074052,-20.8191855580808,
10.337432025741));
#147106=CARTESIAN_POINT('Ctrl Pts',(20.4241713526063,-20.8765664143948,
10.3415971763278));
#147107=CARTESIAN_POINT('Ctrl Pts',(20.3601263754954,-20.9309805713415,
10.3457623269146));
#147108=CARTESIAN_POINT('Ctrl Pts',(20.2935357468249,-20.9821350335323,
10.3499274775013));
#147109=CARTESIAN_POINT('Ctrl Pts',(20.2954164701606,-20.9846205560609,
9.5499633223245));
#147110=CARTESIAN_POINT('Ctrl Pts',(19.6881794406823,-21.4438296808101,
9.58795779884996));
#147111=CARTESIAN_POINT('Ctrl Pts',(17.9381456550696,-21.8241543919292,
9.66834421093588));
#147112=CARTESIAN_POINT('Ctrl Pts',(16.3483940953146,-20.372000527443,9.7627861705977));
#147113=CARTESIAN_POINT('Ctrl Pts',(16.174290432163,-19.2372014285682,9.81923365373404));
#147114=CARTESIAN_POINT('Ctrl Pts',(16.1763511785197,-18.9540199907297,
9.8332892013099));
#147115=CARTESIAN_POINT('',(16.1740010233873,-18.9497109517325,9.7667098901893));
#147116=CARTESIAN_POINT('Ctrl Pts',(20.2935357468249,-20.9821350335323,
9.48328065736197));
#147117=CARTESIAN_POINT('Ctrl Pts',(20.2268468056927,-21.033365018679,9.48745093467704));
#147118=CARTESIAN_POINT('Ctrl Pts',(20.1576478466326,-21.0812925043171,
9.49162121199211));
#147119=CARTESIAN_POINT('Ctrl Pts',(20.0863050736588,-21.1256768360905,
9.49579148930719));
#147120=CARTESIAN_POINT('Ctrl Pts',(20.0148829142921,-21.1701105563565,
9.49996640708211));
#147121=CARTESIAN_POINT('Ctrl Pts',(19.9413125717026,-21.2109930116134,
9.50414132485704));
#147122=CARTESIAN_POINT('Ctrl Pts',(19.8659864837341,-21.2481286115205,
9.50831624263196));
#147123=CARTESIAN_POINT('Ctrl Pts',(19.7906119648809,-21.2852880877501,
9.51249384466897));
#147124=CARTESIAN_POINT('Ctrl Pts',(19.7134798757101,-21.318695731469,9.51667144670598));
#147125=CARTESIAN_POINT('Ctrl Pts',(19.6350021373819,-21.3482043210948,
9.520849048743));
#147126=CARTESIAN_POINT('Ctrl Pts',(19.5563968680676,-21.3777608639314,
9.52503343963145));
#147127=CARTESIAN_POINT('Ctrl Pts',(19.4764420228001,-21.4034055677312,
9.52921783051991));
#147128=CARTESIAN_POINT('Ctrl Pts',(19.3955636713297,-21.4250413479715,
9.53340222140836));
#147129=CARTESIAN_POINT('Ctrl Pts',(19.3647456632446,-21.4332854780539,
9.53499664797477));
#147130=CARTESIAN_POINT('Ctrl Pts',(19.333793658731,-21.4409480748349,9.53659107454117));
#147131=CARTESIAN_POINT('Ctrl Pts',(19.3027314805895,-21.4480257416514,
9.53818550110758));
#147132=CARTESIAN_POINT('Ctrl Pts',(19.2212075887321,-21.4666013528504,
9.54237013550063));
#147133=CARTESIAN_POINT('Ctrl Pts',(19.1386209669249,-21.4812132961356,
9.54655476989368));
#147134=CARTESIAN_POINT('Ctrl Pts',(19.0553917867601,-21.4917455225678,
9.55073940428673));
#147135=CARTESIAN_POINT('Ctrl Pts',(18.9722810730315,-21.5022627576793,
9.55491808237067));
#147136=CARTESIAN_POINT('Ctrl Pts',(18.8885300701227,-21.508711753151,9.55909676045462));
#147137=CARTESIAN_POINT('Ctrl Pts',(18.8045707324915,-21.5110271142986,
9.56327543853857));
#147138=CARTESIAN_POINT('Ctrl Pts',(18.7191064840738,-21.5133839766308,
9.567529016424));
#147139=CARTESIAN_POINT('Ctrl Pts',(18.6334268287618,-21.5114574491382,
9.57178259430944));
#147140=CARTESIAN_POINT('Ctrl Pts',(18.547994628297,-21.5052336363321,9.57603617219488));
#147141=CARTESIAN_POINT('Ctrl Pts',(18.4642186977454,-21.499130484282,9.58020728617283));
#147142=CARTESIAN_POINT('Ctrl Pts',(18.3806811928202,-21.4888952174951,
9.58437840015078));
#147143=CARTESIAN_POINT('Ctrl Pts',(18.2978184502098,-21.4745672747466,
9.58854951412873));
#147144=CARTESIAN_POINT('Ctrl Pts',(18.214983512993,-21.4602441398778,9.5927192284491));
#147145=CARTESIAN_POINT('Ctrl Pts',(18.1328233413403,-21.4418311348331,
9.59688894276948));
#147146=CARTESIAN_POINT('Ctrl Pts',(18.051766797798,-21.4194192707793,9.60105865708985));
#147147=CARTESIAN_POINT('Ctrl Pts',(17.9707131385955,-21.3970082042359,
9.6052282230339));
#147148=CARTESIAN_POINT('Ctrl Pts',(17.8907634725899,-21.3705986850245,
9.60939778897794));
#147149=CARTESIAN_POINT('Ctrl Pts',(17.812332824503,-21.3403319739122,9.61356735492198));
#147150=CARTESIAN_POINT('Ctrl Pts',(17.731144651584,-21.3090011225752,9.6178835176609));
#147151=CARTESIAN_POINT('Ctrl Pts',(17.6515847934176,-21.2735369848542,
9.62219968039982));
#147152=CARTESIAN_POINT('Ctrl Pts',(17.5740906315701,-21.2341503581115,
9.62651584313874));
#147153=CARTESIAN_POINT('Ctrl Pts',(17.4991208338937,-21.1960467465922,
9.63069140733042));
#147154=CARTESIAN_POINT('Ctrl Pts',(17.4260846045832,-21.1542725466306,
9.6348669715221));
#147155=CARTESIAN_POINT('Ctrl Pts',(17.3553508285745,-21.1090643157143,
9.63904253571378));
#147156=CARTESIAN_POINT('Ctrl Pts',(17.2810444576934,-21.0615727245268,
9.64342899772632));
#147157=CARTESIAN_POINT('Ctrl Pts',(17.2092797216844,-21.0102914191919,
9.64781545973885));
#147158=CARTESIAN_POINT('Ctrl Pts',(17.1404457653639,-20.9555430869521,
9.65220192175139));
#147159=CARTESIAN_POINT('Ctrl Pts',(17.0716118090435,-20.9007947547123,
9.65658838376393));
#147160=CARTESIAN_POINT('Ctrl Pts',(17.0057090169082,-20.8425798367027,
9.66097484577646));
#147161=CARTESIAN_POINT('Ctrl Pts',(16.9430809195061,-20.7812645645512,
9.665361307789));
#147162=CARTESIAN_POINT('Ctrl Pts',(16.8827886985014,-20.7222362035939,
9.66958416538901));
#147163=CARTESIAN_POINT('Ctrl Pts',(16.8252872091303,-20.6600954577447,
9.67380702298902));
#147164=CARTESIAN_POINT('Ctrl Pts',(16.7709203169311,-20.5951427685755,
9.67802988058904));
#147165=CARTESIAN_POINT('Ctrl Pts',(16.7179063153622,-20.5318063918538,
9.68214765466763));
#147166=CARTESIAN_POINT('Ctrl Pts',(16.6678730797622,-20.4657967543979,
9.68626542874624));
#147167=CARTESIAN_POINT('Ctrl Pts',(16.6211045875939,-20.3974317611818,
9.69038320282483));
#147168=CARTESIAN_POINT('Ctrl Pts',(16.57438033231,-20.329131432319,9.69449708202704));
#147169=CARTESIAN_POINT('Ctrl Pts',(16.530914960773,-20.2584805564846,9.69861096122925));
#147170=CARTESIAN_POINT('Ctrl Pts',(16.4909521572678,-20.1858299620347,
9.70272484043146));
#147171=CARTESIAN_POINT('Ctrl Pts',(16.4510143565681,-20.11322482157,9.70683614577718));
#147172=CARTESIAN_POINT('Ctrl Pts',(16.4145750025456,-20.0386228602468,
9.71094745112289));
#147173=CARTESIAN_POINT('Ctrl Pts',(16.3818335581792,-19.9624024099199,
9.71505875646861));
#147174=CARTESIAN_POINT('Ctrl Pts',(16.3475554603697,-19.8826047069797,
9.719363017612));
#147175=CARTESIAN_POINT('Ctrl Pts',(16.3173311789842,-19.8010333411257,
9.72366727875539));
#147176=CARTESIAN_POINT('Ctrl Pts',(16.2913340385439,-19.718148158481,9.72797153989879));
#147177=CARTESIAN_POINT('Ctrl Pts',(16.2665001036005,-19.6389715567965,
9.73208321292913));
#147178=CARTESIAN_POINT('Ctrl Pts',(16.245523244682,-19.5585966865051,9.73619488595948));
#147179=CARTESIAN_POINT('Ctrl Pts',(16.2285034541843,-19.4774398718271,
9.74030655898983));
#147180=CARTESIAN_POINT('Ctrl Pts',(16.2114791195104,-19.3962613887933,
9.74441932981084));
#147181=CARTESIAN_POINT('Ctrl Pts',(16.1984140354436,-19.3143010135803,
9.74853210063185));
#147182=CARTESIAN_POINT('Ctrl Pts',(16.1893567554131,-19.2319834955465,
9.75264487145287));
#147183=CARTESIAN_POINT('Ctrl Pts',(16.1802905487374,-19.1495848472745,
9.75676169572549));
#147184=CARTESIAN_POINT('Ctrl Pts',(16.1752400549859,-19.0668288268568,
9.76087851999812));
#147185=CARTESIAN_POINT('Ctrl Pts',(16.1742017924823,-18.9841424452887,
9.76499534427075));
#147186=CARTESIAN_POINT('Ctrl Pts',(16.1740576564023,-18.9726635650768,
9.76556685957694));
#147187=CARTESIAN_POINT('Ctrl Pts',(16.1739907628404,-18.9611860219109,
9.76613837488311));
#147188=CARTESIAN_POINT('Ctrl Pts',(16.1740010233873,-18.9497109517325,
9.7667098901893));
#147189=CARTESIAN_POINT('Ctrl Pts',(16.174001023388,-18.9497109509451,9.76670989022852));
#147190=CARTESIAN_POINT('Ctrl Pts',(16.1741079389015,-18.8301400729777,
9.7726651119283));
#147191=CARTESIAN_POINT('Ctrl Pts',(16.18259555166,-18.7109297707787,9.77862033362807));
#147192=CARTESIAN_POINT('Ctrl Pts',(16.1992930219765,-18.5930285031387,
9.78457555532785));
#147193=CARTESIAN_POINT('Ctrl Pts',(16.2067339930636,-18.5404876147875,
9.78722940837539));
#147194=CARTESIAN_POINT('Ctrl Pts',(16.2158047738385,-18.4882062515533,
9.78988326142292));
#147195=CARTESIAN_POINT('Ctrl Pts',(16.2264874578014,-18.4362666864388,
9.79253711447045));
#147196=CARTESIAN_POINT('Ctrl Pts',(16.2433320704913,-18.3543676186888,
9.7967217488635));
#147197=CARTESIAN_POINT('Ctrl Pts',(16.2642246666771,-18.2731422629635,
9.80090638325655));
#147198=CARTESIAN_POINT('Ctrl Pts',(16.2890969179466,-18.193021133782,9.80509101764959));
#147199=CARTESIAN_POINT('Ctrl Pts',(16.3139337666449,-18.1130140471109,
9.80926969573354));
#147200=CARTESIAN_POINT('Ctrl Pts',(16.3427388836329,-18.0341085006258,
9.81344837381748));
#147201=CARTESIAN_POINT('Ctrl Pts',(16.3753929533287,-17.9567247619916,
9.81762705190143));
#147202=CARTESIAN_POINT('Ctrl Pts',(16.4086323237558,-17.8779539754572,
9.82188062978686));
#147203=CARTESIAN_POINT('Ctrl Pts',(16.4458598919279,-17.8007605624573,
9.8261342076723));
#147204=CARTESIAN_POINT('Ctrl Pts',(16.4868966678982,-17.7255716022299,
9.83038778555773));
#147205=CARTESIAN_POINT('Ctrl Pts',(16.5271378658896,-17.6518403267158,
9.83455889953568));
#147206=CARTESIAN_POINT('Ctrl Pts',(16.5710416613175,-17.5800368994831,
9.83873001351364));
#147207=CARTESIAN_POINT('Ctrl Pts',(16.618391498167,-17.5105421730166,9.8429011274916));
#147208=CARTESIAN_POINT('Ctrl Pts',(16.6657254463214,-17.4410707661768,
9.84707084181197));
#147209=CARTESIAN_POINT('Ctrl Pts',(16.7165028805482,-17.3739069013823,
9.85124055613234));
#147210=CARTESIAN_POINT('Ctrl Pts',(16.7704633948898,-17.3094032751791,
9.85541027045272));
#147211=CARTESIAN_POINT('Ctrl Pts',(16.8244219890848,-17.2449019442917,
9.85957983639676));
#147212=CARTESIAN_POINT('Ctrl Pts',(16.8815631423607,-17.1830610160833,
9.86374940234081));
#147213=CARTESIAN_POINT('Ctrl Pts',(16.9415864376593,-17.1241997862083,
9.86791896828485));
#147214=CARTESIAN_POINT('Ctrl Pts',(17.0037200779738,-17.0632690681041,
9.87223513102377));
#147215=CARTESIAN_POINT('Ctrl Pts',(17.0689419268744,-17.0055318485509,
9.87655129376269));
#147216=CARTESIAN_POINT('Ctrl Pts',(17.1368790142893,-16.9512989836053,
9.88086745650161));
#147217=CARTESIAN_POINT('Ctrl Pts',(17.2026030582275,-16.8988327485311,
9.88504302069329));
#147218=CARTESIAN_POINT('Ctrl Pts',(17.2708677497022,-16.8496463025101,
9.88921858488496));
#147219=CARTESIAN_POINT('Ctrl Pts',(17.3413050297814,-16.8039774861683,
9.89339414907664));
#147220=CARTESIAN_POINT('Ctrl Pts',(17.4152999294287,-16.7560020464804,
9.89778061108918));
#147221=CARTESIAN_POINT('Ctrl Pts',(17.4916921547951,-16.7119092180967,
9.90216707310172));
#147222=CARTESIAN_POINT('Ctrl Pts',(17.5700268579948,-16.6719196231952,
9.90655353511426));
#147223=CARTESIAN_POINT('Ctrl Pts',(17.6483615611944,-16.6319300282936,
9.91093999712679));
#147224=CARTESIAN_POINT('Ctrl Pts',(17.7286381814853,-16.5960438342244,
9.91532645913933));
#147225=CARTESIAN_POINT('Ctrl Pts',(17.8103811197834,-16.5644221134993,
9.91971292115187));
#147226=CARTESIAN_POINT('Ctrl Pts',(17.8883629443183,-16.5342553550193,
9.92389755554492));
#147227=CARTESIAN_POINT('Ctrl Pts',(17.967969380348,-16.5078569775931,9.92808218993797));
#147228=CARTESIAN_POINT('Ctrl Pts',(18.0488014484187,-16.4854025571831,
9.93226682433102));
#147229=CARTESIAN_POINT('Ctrl Pts',(18.1295184620454,-16.4629800978612,
9.93644550241496));
#147230=CARTESIAN_POINT('Ctrl Pts',(18.2114572030593,-16.4444905669892,
9.9406241804989));
#147231=CARTESIAN_POINT('Ctrl Pts',(18.2941997096014,-16.4300611219609,
9.94480285858285));
#147232=CARTESIAN_POINT('Ctrl Pts',(18.3784253161073,-16.4153730395006,
9.94905643646828));
#147233=CARTESIAN_POINT('Ctrl Pts',(18.4634833368927,-16.404892202575,9.95331001435371));
#147234=CARTESIAN_POINT('Ctrl Pts',(18.5489177820416,-16.3986992788558,
9.95756359223915));
#147235=CARTESIAN_POINT('Ctrl Pts',(18.6326959137598,-16.3926264170474,
9.9617347062171));
#147236=CARTESIAN_POINT('Ctrl Pts',(18.7168355246874,-16.3906767277746,
9.96590582019505));
#147237=CARTESIAN_POINT('Ctrl Pts',(18.8008991604927,-16.3928742699263,
9.97007693417301));
#147238=CARTESIAN_POINT('Ctrl Pts',(18.8849345879332,-16.3950710746715,
9.97424664849338));
#147239=CARTESIAN_POINT('Ctrl Pts',(18.96889363139,-16.4014123350032,9.97841636281375));
#147240=CARTESIAN_POINT('Ctrl Pts',(19.0523387760777,-16.4118699986722,
9.98258607713412));
#147241=CARTESIAN_POINT('Ctrl Pts',(19.1357809514291,-16.4223272902127,
9.98675564307817));
#147242=CARTESIAN_POINT('Ctrl Pts',(19.2187088080138,-16.4369006358009,
9.99092520902221));
#147243=CARTESIAN_POINT('Ctrl Pts',(19.3006912586604,-16.4555102609148,
9.99509477496625));
#147244=CARTESIAN_POINT('Ctrl Pts',(19.3855561111354,-16.4747741774902,
9.99941093770517));
#147245=CARTESIAN_POINT('Ctrl Pts',(19.4694073254463,-16.498363368963,10.0037271004441));
#147246=CARTESIAN_POINT('Ctrl Pts',(19.5517816392175,-16.5261324870145,
10.008043263183));
#147247=CARTESIAN_POINT('Ctrl Pts',(19.6314726183819,-16.5529970289662,
10.0122188273747));
#147248=CARTESIAN_POINT('Ctrl Pts',(19.7097810183148,-16.5837731410383,
10.0163943915664));
#147249=CARTESIAN_POINT('Ctrl Pts',(19.7863076293696,-16.6182800825355,
10.0205699557581));
#147250=CARTESIAN_POINT('Ctrl Pts',(19.866699417624,-16.6545298876152,10.0249564177706));
#147251=CARTESIAN_POINT('Ctrl Pts',(19.945124171151,-16.6948970480992,10.0293428797831));
#147252=CARTESIAN_POINT('Ctrl Pts',(20.0211501810795,-16.739118527497,10.0337293417957));
#147253=CARTESIAN_POINT('Ctrl Pts',(20.097176191008,-16.7833400068949,10.0381158038082));
#147254=CARTESIAN_POINT('Ctrl Pts',(20.1708030131039,-16.8314154242948,
10.0425022658208));
#147255=CARTESIAN_POINT('Ctrl Pts',(20.2416377781113,-16.8830320616279,
10.0468887278333));
#147256=CARTESIAN_POINT('Ctrl Pts',(20.3092133305783,-16.9322737409631,
10.0510733622264));
#147257=CARTESIAN_POINT('Ctrl Pts',(20.3744996423274,-16.9849212146565,
10.0552579966194));
#147258=CARTESIAN_POINT('Ctrl Pts',(20.4371331217483,-17.0407340400657,
10.0594426310125));
#147259=CARTESIAN_POINT('Ctrl Pts',(20.4996774501638,-17.096467422826,10.0636213090964));
#147260=CARTESIAN_POINT('Ctrl Pts',(20.5595761060152,-17.1553569045525,
10.0677999871804));
#147261=CARTESIAN_POINT('Ctrl Pts',(20.6164959352303,-17.2171198733511,
10.0719786652643));
#147262=CARTESIAN_POINT('Ctrl Pts',(20.6744360114766,-17.2799898989772,
10.0762322431497));
#147263=CARTESIAN_POINT('Ctrl Pts',(20.7292890301008,-17.3458371554909,
10.0804858210352));
#147264=CARTESIAN_POINT('Ctrl Pts',(20.780740343664,-17.414321891416,10.0847393989206));
#147265=CARTESIAN_POINT('Ctrl Pts',(20.8311941731147,-17.4814789170983,
10.0889105128986));
#147266=CARTESIAN_POINT('Ctrl Pts',(20.8783767288093,-17.5511716846818,
10.0930816268765));
#147267=CARTESIAN_POINT('Ctrl Pts',(20.9220309952968,-17.6230453869223,
10.0972527408545));
#147268=CARTESIAN_POINT('Ctrl Pts',(20.9656706131735,-17.6948949712478,
10.1014224551748));
#147269=CARTESIAN_POINT('Ctrl Pts',(21.0057840545747,-17.7689236439344,
10.1055921694952));
#147270=CARTESIAN_POINT('Ctrl Pts',(21.0421580885473,-17.8447483401351,
10.1097618838156));
#147271=CARTESIAN_POINT('Ctrl Pts',(21.0785308281757,-17.9205703381677,
10.1139314497596));
#147272=CARTESIAN_POINT('Ctrl Pts',(21.1111642267361,-17.9981878174991,
10.1181010157037));
#147273=CARTESIAN_POINT('Ctrl Pts',(21.1398920226672,-18.0771951216034,
10.1222705816477));
#147274=CARTESIAN_POINT('Ctrl Pts',(21.1696298524636,-18.158980225054,10.1265867443866));
#147275=CARTESIAN_POINT('Ctrl Pts',(21.1951821474479,-18.242254208487,10.1309029071256));
#147276=CARTESIAN_POINT('Ctrl Pts',(21.2164203674168,-18.326548867269,10.1352190698645));
#147277=CARTESIAN_POINT('Ctrl Pts',(21.236966754604,-18.4080976364075,10.1393946340562));
#147278=CARTESIAN_POINT('Ctrl Pts',(21.2534757664241,-18.4906011339277,
10.1435701982478));
#147279=CARTESIAN_POINT('Ctrl Pts',(21.2658832925888,-18.5736258561825,
10.1477457624395));
#147280=CARTESIAN_POINT('Ctrl Pts',(21.278917493404,-18.6608439597858,10.1521322244521));
#147281=CARTESIAN_POINT('Ctrl Pts',(21.2874249313198,-18.748636744862,10.1565186864646));
#147282=CARTESIAN_POINT('Ctrl Pts',(21.291393102574,-18.8364988359062,10.1609051484772));
#147283=CARTESIAN_POINT('Ctrl Pts',(21.2953612738282,-18.9243609269505,
10.1652916104897));
#147284=CARTESIAN_POINT('Ctrl Pts',(21.294790258252,-19.012291744252,10.1696780725022));
#147285=CARTESIAN_POINT('Ctrl Pts',(21.2897303495757,-19.0997916785801,
10.1740645345148));
#147286=CARTESIAN_POINT('Ctrl Pts',(21.2849027735543,-19.1832739332733,
10.1782495861008));
#147287=CARTESIAN_POINT('Ctrl Pts',(21.2759715218877,-19.266674774493,10.1824346376867));
#147288=CARTESIAN_POINT('Ctrl Pts',(21.2629419677491,-19.3495582017232,
10.1866196892727));
#147289=CARTESIAN_POINT('Ctrl Pts',(21.2499348195042,-19.4322991008789,
10.1907975441565));
#147290=CARTESIAN_POINT('Ctrl Pts',(21.2328434536032,-19.5145239047262,
10.1949753990403));
#147291=CARTESIAN_POINT('Ctrl Pts',(21.2117251381579,-19.5957997668066,
10.1991532539241));
#147292=CARTESIAN_POINT('Ctrl Pts',(21.1906274886257,-19.6769960941389,
10.2033270204521));
#147293=CARTESIAN_POINT('Ctrl Pts',(21.1655108283406,-19.7572448807651,
10.2075007869801));
#147294=CARTESIAN_POINT('Ctrl Pts',(21.1364836587684,-19.8361223158311,
10.2116745535082));
#147295=CARTESIAN_POINT('Ctrl Pts',(21.1074761860977,-19.9149462272128,
10.2158454878528));
#147296=CARTESIAN_POINT('Ctrl Pts',(21.0745636328025,-19.9924002048068,
10.2200164221975));
#147297=CARTESIAN_POINT('Ctrl Pts',(21.0379042545248,-20.0680757975973,
10.2241873565421));
#147298=CARTESIAN_POINT('Ctrl Pts',(21.00125875479,-20.1437227410485,10.2283567118504));
#147299=CARTESIAN_POINT('Ctrl Pts',(20.9608694496218,-20.2175922243102,
10.2325260671587));
#147300=CARTESIAN_POINT('Ctrl Pts',(20.9169420720101,-20.2892972407989,
10.236695422467));
#147301=CARTESIAN_POINT('Ctrl Pts',(20.8729998723142,-20.3610264521712,
10.2408661846094));
#147302=CARTESIAN_POINT('Ctrl Pts',(20.8255174487911,-20.4305893408782,
10.2450369467519));
#147303=CARTESIAN_POINT('Ctrl Pts',(20.7747452964174,-20.4976256452162,
10.2492077088943));
#147304=CARTESIAN_POINT('Ctrl Pts',(20.7239654366853,-20.5646721258578,
10.2533791041704));
#147305=CARTESIAN_POINT('Ctrl Pts',(20.6698951413565,-20.6291908988708,
10.2575504994465));
#147306=CARTESIAN_POINT('Ctrl Pts',(20.6128256045793,-20.690854320401,10.2617218947226));
#147307=CARTESIAN_POINT('Ctrl Pts',(20.5556935666862,-20.7525852741537,
10.2658978584056));
#147308=CARTESIAN_POINT('Ctrl Pts',(20.49555604941,-20.8114543016472,10.2700738220885));
#147309=CARTESIAN_POINT('Ctrl Pts',(20.4327411706605,-20.8671706020882,
10.2742497857714));
#147310=CARTESIAN_POINT('Ctrl Pts',(20.3876731383385,-20.9071455901663,
10.2772459304744));
#147311=CARTESIAN_POINT('Ctrl Pts',(20.3412276536165,-20.9454984392925,
10.2802420751774));
#147312=CARTESIAN_POINT('Ctrl Pts',(20.2935357468249,-20.9821350335323,
10.2832382198805));
#147313=CARTESIAN_POINT('Origin',(18.734,-18.952,-1.76670989022851));
#147314=CARTESIAN_POINT('',(20.2922817658078,-20.9805345212666,11.1497835179515));
#147315=CARTESIAN_POINT('',(20.2948050232964,-20.9838171774959,11.0834063370138));
#147316=CARTESIAN_POINT('',(20.2935357468249,-20.9821350335323,-1.76670989022851));
#147317=CARTESIAN_POINT('',(16.1740004874608,-18.9504201902088,10.6332901097715));
#147318=CARTESIAN_POINT('Ctrl Pts',(16.1772048604514,-18.9504028912009,
10.6332910657491));
#147319=CARTESIAN_POINT('Ctrl Pts',(16.1753928930938,-18.6273578295265,
10.6493117789502));
#147320=CARTESIAN_POINT('Ctrl Pts',(16.3822354976306,-17.4517521542537,
10.7077244277117));
#147321=CARTESIAN_POINT('Ctrl Pts',(18.1490152356806,-15.9819691251248,
10.8085290120338));
#147322=CARTESIAN_POINT('Ctrl Pts',(20.9146847903814,-16.8524990075743,
10.9357048187152));
#147323=CARTESIAN_POINT('Ctrl Pts',(21.5989574361765,-19.3539801738065,
11.0494563206878));
#147324=CARTESIAN_POINT('Ctrl Pts',(20.7519189177889,-20.6211556360716,
11.1208158870999));
#147325=CARTESIAN_POINT('Ctrl Pts',(20.292281765808,-20.9805345212664,11.1497835179515));
#147326=CARTESIAN_POINT('Ctrl Pts',(20.2935357468249,-20.9821350335323,
10.3499274775013));
#147327=CARTESIAN_POINT('Ctrl Pts',(20.2268718913476,-21.0333457480517,
10.3540972083223));
#147328=CARTESIAN_POINT('Ctrl Pts',(20.1576571264186,-21.0812892905445,
10.3582669391434));
#147329=CARTESIAN_POINT('Ctrl Pts',(20.086248880528,-21.1257117943993,10.3624366699644));
#147330=CARTESIAN_POINT('Ctrl Pts',(20.0148436247903,-21.1701324381037,
10.3666062261818));
#147331=CARTESIAN_POINT('Ctrl Pts',(19.9412454617371,-21.2110320939803,
10.3707757823993));
#147332=CARTESIAN_POINT('Ctrl Pts',(19.8658394210623,-21.2482011072486,
10.3749453386168));
#147333=CARTESIAN_POINT('Ctrl Pts',(19.7873867082221,-21.2868718808152,
10.3792833597312));
#147334=CARTESIAN_POINT('Ctrl Pts',(19.7069774009645,-21.3215038936756,
10.3836213808456));
#147335=CARTESIAN_POINT('Ctrl Pts',(19.6250697922386,-21.351915545464,10.38795940196));
#147336=CARTESIAN_POINT('Ctrl Pts',(19.5462303075402,-21.3811880268991,
10.3921349279531));
#147337=CARTESIAN_POINT('Ctrl Pts',(19.4660032377296,-21.406550602145,10.3963104539462));
#147338=CARTESIAN_POINT('Ctrl Pts',(19.3848125515317,-21.4278923689791,
10.4004859799393));
#147339=CARTESIAN_POINT('Ctrl Pts',(19.3035638143394,-21.4492493950854,
10.4046644914157));
#147340=CARTESIAN_POINT('Ctrl Pts',(19.2213505391032,-21.4665797981134,
10.4088430028921));
#147341=CARTESIAN_POINT('Ctrl Pts',(19.138605750157,-21.4798240023664,10.4130215143685));
#147342=CARTESIAN_POINT('Ctrl Pts',(19.0557327305457,-21.4930887313334,
10.417206501338));
#147343=CARTESIAN_POINT('Ctrl Pts',(18.9723270098871,-21.5022545827837,
10.4213914883074));
#147344=CARTESIAN_POINT('Ctrl Pts',(18.8888248918782,-21.5073139245218,
10.4255764752769));
#147345=CARTESIAN_POINT('Ctrl Pts',(18.8793465458456,-21.5078882116517,
10.4260515141811));
#147346=CARTESIAN_POINT('Ctrl Pts',(18.8698669547576,-21.5084096433106,
10.4265265530853));
#147347=CARTESIAN_POINT('Ctrl Pts',(18.8603867536229,-21.5088782506229,
10.4270015919895));
#147348=CARTESIAN_POINT('Ctrl Pts',(18.7768753288336,-21.5130062288976,
10.4311862263825));
#147349=CARTESIAN_POINT('Ctrl Pts',(18.6930060412949,-21.5130461767751,
10.4353708607756));
#147350=CARTESIAN_POINT('Ctrl Pts',(18.6092128353627,-21.5089568169099,
10.4395554951686));
#147351=CARTESIAN_POINT('Ctrl Pts',(18.5255388986879,-21.5048732777423,
10.4437341732525));
#147352=CARTESIAN_POINT('Ctrl Pts',(18.4419412840721,-21.4966721277452,
10.4479128513365));
#147353=CARTESIAN_POINT('Ctrl Pts',(18.3588567381423,-21.48436402065,10.4520915294204));
#147354=CARTESIAN_POINT('Ctrl Pts',(18.274282961438,-21.4718352995808,10.4563451073058));
#147355=CARTESIAN_POINT('Ctrl Pts',(18.1902413094011,-21.4550509150076,
10.4605986851913));
#147356=CARTESIAN_POINT('Ctrl Pts',(18.1071900176379,-21.4340776067664,
10.4648522630767));
#147357=CARTESIAN_POINT('Ctrl Pts',(18.025748837227,-21.4135109070316,10.4690233770546));
#147358=CARTESIAN_POINT('Ctrl Pts',(17.9452604262043,-21.3889163729568,
10.4731944910326));
#147359=CARTESIAN_POINT('Ctrl Pts',(17.8661476315636,-21.3604086585543,
10.4773656050105));
#147360=CARTESIAN_POINT('Ctrl Pts',(17.7870613839853,-21.3319105101907,
10.4815353193309));
#147361=CARTESIAN_POINT('Ctrl Pts',(17.7093502684731,-21.2995019451713,
10.4857050336513));
#147362=CARTESIAN_POINT('Ctrl Pts',(17.6334208106706,-21.2633471067789,
10.4898747479716));
#147363=CARTESIAN_POINT('Ctrl Pts',(17.5574940547643,-21.2271935549308,
10.4940443139157));
#147364=CARTESIAN_POINT('Ctrl Pts',(17.4833492454977,-21.1872941933052,
10.4982138798597));
#147365=CARTESIAN_POINT('Ctrl Pts',(17.4113705501186,-21.143860246071,10.5023834458037));
#147366=CARTESIAN_POINT('Ctrl Pts',(17.3368611726046,-21.0988992148333,
10.5066996085427));
#147367=CARTESIAN_POINT('Ctrl Pts',(17.2646735157637,-21.0501506938751,
10.5110157712816));
#147368=CARTESIAN_POINT('Ctrl Pts',(17.195201681377,-20.9978982708344,10.5153319340205));
#147369=CARTESIAN_POINT('Ctrl Pts',(17.1279928846885,-20.9473479649783,
10.5195074982122));
#147370=CARTESIAN_POINT('Ctrl Pts',(17.0633260236122,-20.8935188682657,
10.5236830624039));
#147371=CARTESIAN_POINT('Ctrl Pts',(17.0015232692744,-20.8367080350798,
10.5278586265956));
#147372=CARTESIAN_POINT('Ctrl Pts',(16.9365990047368,-20.7770278217644,
10.5322450886081));
#147373=CARTESIAN_POINT('Ctrl Pts',(16.8748361916365,-20.714057157727,10.5366315506207));
#147374=CARTESIAN_POINT('Ctrl Pts',(16.8165619874416,-20.6481814372278,
10.5410180126332));
#147375=CARTESIAN_POINT('Ctrl Pts',(16.7582877832468,-20.5823057167286,
10.5454044746458));
#147376=CARTESIAN_POINT('Ctrl Pts',(16.7035024899566,-20.5135254410002,
10.5497909366583));
#147377=CARTESIAN_POINT('Ctrl Pts',(16.6524807786035,-20.4422609606901,
10.5541773986709));
#147378=CARTESIAN_POINT('Ctrl Pts',(16.6033728384837,-20.3736695367859,
10.5583993290636));
#147379=CARTESIAN_POINT('Ctrl Pts',(16.55756917535,-20.302523084569,10.5626212594563));
#147380=CARTESIAN_POINT('Ctrl Pts',(16.5153433201942,-20.2291697370175,
10.5668431898491));
#147381=CARTESIAN_POINT('Ctrl Pts',(16.4731798646836,-20.1559247880487,
10.5710588812454));
#147382=CARTESIAN_POINT('Ctrl Pts',(16.4345839361667,-20.0804798079436,
10.5752745726417));
#147383=CARTESIAN_POINT('Ctrl Pts',(16.3997870211452,-20.0032134746785,
10.579490264038));
#147384=CARTESIAN_POINT('Ctrl Pts',(16.3650317212897,-19.9260395476307,
10.583700913703));
#147385=CARTESIAN_POINT('Ctrl Pts',(16.3340665899187,-19.8470490030815,
10.587911563368));
#147386=CARTESIAN_POINT('Ctrl Pts',(16.3070776023617,-19.7666457364042,
10.5921222130329));
#147387=CARTESIAN_POINT('Ctrl Pts',(16.2801155537111,-19.686322723796,10.5963286598616));
#147388=CARTESIAN_POINT('Ctrl Pts',(16.2571218975387,-19.6045902181233,
10.6005351066902));
#147389=CARTESIAN_POINT('Ctrl Pts',(16.2382342921444,-19.5218715043693,
10.6047415535189));
#147390=CARTESIAN_POINT('Ctrl Pts',(16.2193575415102,-19.439200329293,10.6089455828907));
#147391=CARTESIAN_POINT('Ctrl Pts',(16.2045822501753,-19.3555445100533,
10.6131496122625));
#147392=CARTESIAN_POINT('Ctrl Pts',(16.1939957867901,-19.271340878805,10.6173536416343));
#147393=CARTESIAN_POINT('Ctrl Pts',(16.1834116610727,-19.1871558411241,
10.6215567426862));
#147394=CARTESIAN_POINT('Ctrl Pts',(16.1770145819502,-19.1024236771961,
10.6257598437382));
#147395=CARTESIAN_POINT('Ctrl Pts',(16.1748403468597,-19.0175886403178,
10.6299629447901));
#147396=CARTESIAN_POINT('Ctrl Pts',(16.1742666403856,-18.9952035679304,
10.6310719997839));
#147397=CARTESIAN_POINT('Ctrl Pts',(16.1739866695752,-18.9728113543428,
10.6321810547777));
#147398=CARTESIAN_POINT('Ctrl Pts',(16.1740004874608,-18.9504201902088,
10.6332901097715));
#147399=CARTESIAN_POINT('',(16.1739802850659,-18.9533010441961,10.5667098967402));
#147400=CARTESIAN_POINT('Ctrl Pts',(20.2935357468249,-20.9821350335323,
10.2832382198805));
#147401=CARTESIAN_POINT('Ctrl Pts',(20.2269313188769,-21.0333000962331,
10.2874225043308));
#147402=CARTESIAN_POINT('Ctrl Pts',(20.1578951114202,-21.081115850127,10.2916067887811));
#147403=CARTESIAN_POINT('Ctrl Pts',(20.0868063431064,-21.1253649021853,
10.2957910732315));
#147404=CARTESIAN_POINT('Ctrl Pts',(20.0559462878668,-21.1445736776812,
10.2976074958864));
#147405=CARTESIAN_POINT('Ctrl Pts',(20.0246997331957,-21.1631109097862,
10.2994239185413));
#147406=CARTESIAN_POINT('Ctrl Pts',(19.9930989518198,-21.1809616034213,
10.3012403411962));
#147407=CARTESIAN_POINT('Ctrl Pts',(19.9202977696528,-21.2220856371494,
10.3054249755893));
#147408=CARTESIAN_POINT('Ctrl Pts',(19.845344231219,-21.2597157589185,10.3096096099823));
#147409=CARTESIAN_POINT('Ctrl Pts',(19.7686077403709,-21.2936205549928,
10.3137942443753));
#147410=CARTESIAN_POINT('Ctrl Pts',(19.6919804744194,-21.3274770917864,
10.3179729224593));
#147411=CARTESIAN_POINT('Ctrl Pts',(19.6135757141378,-21.3576186510691,
10.3221516005432));
#147412=CARTESIAN_POINT('Ctrl Pts',(19.5337886464593,-21.3838589846031,
10.3263302786272));
#147413=CARTESIAN_POINT('Ctrl Pts',(19.4525714529346,-21.410569657257,10.3305838565126));
#147414=CARTESIAN_POINT('Ctrl Pts',(19.3699223286581,-21.43323763244,10.334837434398));
#147415=CARTESIAN_POINT('Ctrl Pts',(19.2862808103368,-21.4517171653077,
10.3390910122835));
#147416=CARTESIAN_POINT('Ctrl Pts',(19.2042608460611,-21.4698384363709,
10.3432621262614));
#147417=CARTESIAN_POINT('Ctrl Pts',(19.1212870932383,-21.4839321143086,
10.3474332402394));
#147418=CARTESIAN_POINT('Ctrl Pts',(19.0377889319357,-21.4939111480997,
10.3516043542173));
#147419=CARTESIAN_POINT('Ctrl Pts',(18.9543187892475,-21.5038868333295,
10.3557740685377));
#147420=CARTESIAN_POINT('Ctrl Pts',(18.8703250439617,-21.5097505619763,
10.3599437828581));
#147421=CARTESIAN_POINT('Ctrl Pts',(18.7862446699246,-21.5114668379302,
10.3641134971784));
#147422=CARTESIAN_POINT('Ctrl Pts',(18.702167287828,-21.5131830528116,10.3682830631225));
#147423=CARTESIAN_POINT('Ctrl Pts',(18.6180037430636,-21.510752099899,10.3724526290665));
#147424=CARTESIAN_POINT('Ctrl Pts',(18.5341921271334,-21.5041905912256,
10.3766221950106));
#147425=CARTESIAN_POINT('Ctrl Pts',(18.44743379818,-21.4973983880017,10.3809383577495));
#147426=CARTESIAN_POINT('Ctrl Pts',(18.3610531319647,-21.4861798052051,
10.3852545204884));
#147427=CARTESIAN_POINT('Ctrl Pts',(18.2755295374792,-21.470611688013,10.3895706832273));
#147428=CARTESIAN_POINT('Ctrl Pts',(18.1927918650885,-21.4555507006011,
10.393746247419));
#147429=CARTESIAN_POINT('Ctrl Pts',(18.1108567316686,-21.4364193523526,
10.3979218116107));
#147430=CARTESIAN_POINT('Ctrl Pts',(18.0301452832766,-21.4133387693989,
10.4020973758024));
#147431=CARTESIAN_POINT('Ctrl Pts',(17.9453572914996,-21.3890924410691,
10.4064838378149));
#147432=CARTESIAN_POINT('Ctrl Pts',(17.8619204024431,-21.3604876310562,
10.4108702998275));
#147433=CARTESIAN_POINT('Ctrl Pts',(17.7802998178502,-21.3277221981047,
10.41525676184));
#147434=CARTESIAN_POINT('Ctrl Pts',(17.6986792332574,-21.2949567651532,
10.4196432238525));
#147435=CARTESIAN_POINT('Ctrl Pts',(17.6188754477654,-21.258031021948,10.4240296858651));
#147436=CARTESIAN_POINT('Ctrl Pts',(17.5413224142635,-21.2171976020828,
10.4284161478776));
#147437=CARTESIAN_POINT('Ctrl Pts',(17.4673377107943,-21.1782429883953,
10.4326007822707));
#147438=CARTESIAN_POINT('Ctrl Pts',(17.3951258047344,-21.135587395429,10.4367854166637));
#147439=CARTESIAN_POINT('Ctrl Pts',(17.3250812297128,-21.0894161734984,
10.4409700510568));
#147440=CARTESIAN_POINT('Ctrl Pts',(17.255136354474,-21.0433106705873,10.4451487291407));
#147441=CARTESIAN_POINT('Ctrl Pts',(17.1873530634459,-20.9936997293727,
10.4493274072247));
#147442=CARTESIAN_POINT('Ctrl Pts',(17.1221018691138,-20.940814826887,10.4535060853086));
#147443=CARTESIAN_POINT('Ctrl Pts',(17.0556810940184,-20.8869820005319,
10.457759663194));
#147444=CARTESIAN_POINT('Ctrl Pts',(16.9918845107681,-20.8297569115571,
10.4620132410795));
#147445=CARTESIAN_POINT('Ctrl Pts',(16.9310725805954,-20.7694302518554,
10.4662668189649));
#147446=CARTESIAN_POINT('Ctrl Pts',(16.8714396083538,-20.7102731421697,
10.4704379329429));
#147447=CARTESIAN_POINT('Ctrl Pts',(16.8146769368997,-20.6481339874867,
10.4746090469208));
#147448=CARTESIAN_POINT('Ctrl Pts',(16.7610901776525,-20.5833267094255,
10.4787801608988));
#147449=CARTESIAN_POINT('Ctrl Pts',(16.70752139996,-20.5185411780723,10.4829498752191));
#147450=CARTESIAN_POINT('Ctrl Pts',(16.6571267108674,-20.4510896556874,
10.4871195895395));
#147451=CARTESIAN_POINT('Ctrl Pts',(16.6101724826409,-20.3813203547519,
10.4912893038599));
#147452=CARTESIAN_POINT('Ctrl Pts',(16.5632199252473,-20.3115535365076,
10.4954588698039));
#147453=CARTESIAN_POINT('Ctrl Pts',(16.5197078414471,-20.2394694858256,
10.499628435748));
#147454=CARTESIAN_POINT('Ctrl Pts',(16.4798593937702,-20.1654455601081,
10.503798001692));
#147455=CARTESIAN_POINT('Ctrl Pts',(16.4386099238314,-20.0888190444807,
10.5081141644309));
#147456=CARTESIAN_POINT('Ctrl Pts',(16.4012867603007,-20.0101141681399,
10.5124303271699));
#147457=CARTESIAN_POINT('Ctrl Pts',(16.3680847835395,-19.9297756330165,
10.5167464899088));
#147458=CARTESIAN_POINT('Ctrl Pts',(16.3359643576791,-19.8520541172246,
10.5209220541005));
#147459=CARTESIAN_POINT('Ctrl Pts',(16.307700860257,-19.7728042005823,10.5250976182921));
#147460=CARTESIAN_POINT('Ctrl Pts',(16.2834204017388,-19.6924455635533,
10.5292731824838));
#147461=CARTESIAN_POINT('Ctrl Pts',(16.257913594982,-19.6080282028025,10.5336596444963));
#147462=CARTESIAN_POINT('Ctrl Pts',(16.236802907853,-19.522387742153,10.5380461065089));
#147463=CARTESIAN_POINT('Ctrl Pts',(16.2201737773397,-19.4360224398369,
10.5424325685214));
#147464=CARTESIAN_POINT('Ctrl Pts',(16.2035446468265,-19.3496571375208,
10.546819030534));
#147465=CARTESIAN_POINT('Ctrl Pts',(16.1913970777482,-19.2625675787001,
10.5512054925465));
#147466=CARTESIAN_POINT('Ctrl Pts',(16.1837535357011,-19.1752553948527,
10.555591954559));
#147467=CARTESIAN_POINT('Ctrl Pts',(16.1772957565522,-19.1014881810632,
10.5592979331155));
#147468=CARTESIAN_POINT('Ctrl Pts',(16.174038011382,-19.0274367677245,10.563003911672));
#147469=CARTESIAN_POINT('Ctrl Pts',(16.1740003306697,-18.9533011644427,
10.5667098902285));
#147470=CARTESIAN_POINT('Ctrl Pts',(16.1705864007212,-18.9532806854788,
10.5667109992167));
#147471=CARTESIAN_POINT('Ctrl Pts',(16.1754042043383,-18.178366800346,10.6053965865579));
#147472=CARTESIAN_POINT('Ctrl Pts',(16.9631831042392,-16.5458334607307,
10.6864741094597));
#147473=CARTESIAN_POINT('Ctrl Pts',(19.7422306997689,-16.0977465603627,
10.8099435679219));
#147474=CARTESIAN_POINT('Ctrl Pts',(21.6797116025125,-18.2548092108606,
10.9371193746034));
#147475=CARTESIAN_POINT('Ctrl Pts',(21.1313727461762,-20.2593600726663,
11.0282736309673));
#147476=CARTESIAN_POINT('Ctrl Pts',(20.3968579082113,-20.906920109619,11.0770359517708));
#147477=CARTESIAN_POINT('Ctrl Pts',(20.2948050232963,-20.9838171774959,
11.0834063370138));
#147478=CARTESIAN_POINT('Origin',(18.734,-18.952,-1.76670989022851));
#147479=CARTESIAN_POINT('',(20.2935357468249,-20.9821350335323,11.9498687307687));
#147480=CARTESIAN_POINT('',(20.2935357468249,-20.9821350335323,11.8833305117342));
#147481=CARTESIAN_POINT('',(20.2935357468249,-20.9821350335323,-1.76670989022851));
#147482=CARTESIAN_POINT('',(16.1739804747524,-18.9506989546656,11.4332901033215));
#147483=CARTESIAN_POINT('Ctrl Pts',(16.1740003306697,-18.950698835557,11.4332901097715));
#147484=CARTESIAN_POINT('Ctrl Pts',(16.174038011382,-18.8765632322752,11.436996088328));
#147485=CARTESIAN_POINT('Ctrl Pts',(16.1772957565522,-18.8025118189363,
11.4407020668845));
#147486=CARTESIAN_POINT('Ctrl Pts',(16.1837535357011,-18.7287446051466,
11.444408045441));
#147487=CARTESIAN_POINT('Ctrl Pts',(16.1910453870482,-18.6454497843057,
11.448592679834));
#147488=CARTESIAN_POINT('Ctrl Pts',(16.2024358975503,-18.5623575749321,
11.4527773142271));
#147489=CARTESIAN_POINT('Ctrl Pts',(16.217906819526,-18.4799034980302,11.4569619486201));
#147490=CARTESIAN_POINT('Ctrl Pts',(16.2333557205591,-18.3975667843009,
11.4611406267041));
#147491=CARTESIAN_POINT('Ctrl Pts',(16.2528734125179,-18.3158668471442,
11.465319304788));
#147492=CARTESIAN_POINT('Ctrl Pts',(16.2763898192684,-18.2352349062878,
11.469497982872));
#147493=CARTESIAN_POINT('Ctrl Pts',(16.3003277407088,-18.1531576958409,
11.4737515607574));
#147494=CARTESIAN_POINT('Ctrl Pts',(16.3284090988417,-18.0721876262597,
11.4780051386428));
#147495=CARTESIAN_POINT('Ctrl Pts',(16.3605053261112,-17.9927695620856,
11.4822587165282));
#147496=CARTESIAN_POINT('Ctrl Pts',(16.3919793053844,-17.9148911720571,
11.4864298305062));
#147497=CARTESIAN_POINT('Ctrl Pts',(16.4273136905277,-17.8385055933013,
11.4906009444841));
#147498=CARTESIAN_POINT('Ctrl Pts',(16.4663372697809,-17.7640161019714,
11.4947720584621));
#147499=CARTESIAN_POINT('Ctrl Pts',(16.5053477542952,-17.6895516063097,
11.4989417727825));
#147500=CARTESIAN_POINT('Ctrl Pts',(16.5480447610381,-17.6169823416312,
11.5031114871028));
#147501=CARTESIAN_POINT('Ctrl Pts',(16.5942102750742,-17.5466886704001,
11.5072812014232));
#147502=CARTESIAN_POINT('Ctrl Pts',(16.6403741463431,-17.4763975005194,
11.5114507673673));
#147503=CARTESIAN_POINT('Ctrl Pts',(16.6900060262586,-17.4083821471394,
11.5156203333113));
#147504=CARTESIAN_POINT('Ctrl Pts',(16.7428443053793,-17.3429944065419,
11.5197898992553));
#147505=CARTESIAN_POINT('Ctrl Pts',(16.7975403132107,-17.2753077136495,
11.5241060619943));
#147506=CARTESIAN_POINT('Ctrl Pts',(16.8556720579014,-17.2104372553887,
11.5284222247332));
#147507=CARTESIAN_POINT('Ctrl Pts',(16.9169048877879,-17.1487348078625,
11.5327383874721));
#147508=CARTESIAN_POINT('Ctrl Pts',(16.9761430646814,-17.0890423110745,
11.5369139516638));
#147509=CARTESIAN_POINT('Ctrl Pts',(17.0382830139764,-17.0323148814136,
11.5410895158555));
#147510=CARTESIAN_POINT('Ctrl Pts',(17.1029865459476,-16.9788312001503,
11.5452650800471));
#147511=CARTESIAN_POINT('Ctrl Pts',(17.1709580995006,-16.9226461852919,
11.5496515420597));
#147512=CARTESIAN_POINT('Ctrl Pts',(17.2417585461137,-16.8700415621994,
11.5540380040722));
#147513=CARTESIAN_POINT('Ctrl Pts',(17.3149615008575,-16.8212889126042,
11.5584244660848));
#147514=CARTESIAN_POINT('Ctrl Pts',(17.3881644556012,-16.772536263009,11.5628109280973));
#147515=CARTESIAN_POINT('Ctrl Pts',(17.4637693807619,-16.7276358177823,
11.5671973901098));
#147516=CARTESIAN_POINT('Ctrl Pts',(17.5413224142637,-16.6868023979171,
11.5715838521224));
#147517=CARTESIAN_POINT('Ctrl Pts',(17.615307117733,-16.6478477842295,11.5757684865154));
#147518=CARTESIAN_POINT('Ctrl Pts',(17.6913399834857,-16.6124491640088,
11.5799531209085));
#147519=CARTESIAN_POINT('Ctrl Pts',(17.7690449301558,-16.5808269331021,
11.5841377553015));
#147520=CARTESIAN_POINT('Ctrl Pts',(17.8466392734524,-16.549249712527,11.5883164333855));
#147521=CARTESIAN_POINT('Ctrl Pts',(17.9259005477808,-16.5214383763015,
11.5924951114694));
#147522=CARTESIAN_POINT('Ctrl Pts',(18.0064282347098,-16.4975674125468,
11.5966737895534));
#147523=CARTESIAN_POINT('Ctrl Pts',(18.0883993225526,-16.4732685789225,
11.6009273674388));
#147524=CARTESIAN_POINT('Ctrl Pts',(18.1716822438314,-16.4530529941954,
11.6051809453242));
#147525=CARTESIAN_POINT('Ctrl Pts',(18.2558333466885,-16.4370533501362,
11.6094345232097));
#147526=CARTESIAN_POINT('Ctrl Pts',(18.3383530162095,-16.4213638903979,
11.6136056371876));
#147527=CARTESIAN_POINT('Ctrl Pts',(18.4217070321717,-16.4097284515022,
11.6177767511656));
#147528=CARTESIAN_POINT('Ctrl Pts',(18.5054636294717,-16.4022213571869,
11.6219478651435));
#147529=CARTESIAN_POINT('Ctrl Pts',(18.5891921214365,-16.3947167819496,
11.6261175794639));
#147530=CARTESIAN_POINT('Ctrl Pts',(18.6733224686331,-16.3913378410871,
11.6302872937843));
#147531=CARTESIAN_POINT('Ctrl Pts',(18.7574168390734,-16.3921071015279,
11.6344570081047));
#147532=CARTESIAN_POINT('Ctrl Pts',(18.8415082170751,-16.3928763345952,
11.6386265740487));
#147533=CARTESIAN_POINT('Ctrl Pts',(18.92556316086,-16.3977934704174,11.6427961399927));
#147534=CARTESIAN_POINT('Ctrl Pts',(19.0091442611991,-16.4068289575101,
11.6469657059368));
#147535=CARTESIAN_POINT('Ctrl Pts',(19.0956639699176,-16.4161821211824,
11.6512818686757));
#147536=CARTESIAN_POINT('Ctrl Pts',(19.1816753701877,-16.4299485702282,
11.6555980314146));
#147537=CARTESIAN_POINT('Ctrl Pts',(19.2667015333783,-16.4480373252909,
11.6599141941536));
#147538=CARTESIAN_POINT('Ctrl Pts',(19.3489579782461,-16.46553684106,11.6640897583452));
#147539=CARTESIAN_POINT('Ctrl Pts',(19.4302919452567,-16.4870812228023,
11.6682653225369));
#147540=CARTESIAN_POINT('Ctrl Pts',(19.5102860518794,-16.5125369513646,
11.6724408867286));
#147541=CARTESIAN_POINT('Ctrl Pts',(19.5943204706598,-16.5392783882614,
11.6768273487411));
#147542=CARTESIAN_POINT('Ctrl Pts',(19.6768755727334,-16.570336474695,11.6812138107537));
#147543=CARTESIAN_POINT('Ctrl Pts',(19.7574922067679,-16.605499690457,11.6856002727662));
#147544=CARTESIAN_POINT('Ctrl Pts',(19.8381088408023,-16.640662906219,11.6899867347788));
#147545=CARTESIAN_POINT('Ctrl Pts',(19.9167865216171,-16.6799309241434,
11.6943731967913));
#147546=CARTESIAN_POINT('Ctrl Pts',(19.9930989518199,-16.7230383965788,
11.6987596588038));
#147547=CARTESIAN_POINT('Ctrl Pts',(20.0659001339868,-16.7641624303068,
11.7029442931969));
#147548=CARTESIAN_POINT('Ctrl Pts',(20.1368199197938,-16.8089334362054,
11.7071289275899));
#147549=CARTESIAN_POINT('Ctrl Pts',(20.2054694255015,-16.8571544854538,
11.711313561983));
#147550=CARTESIAN_POINT('Ctrl Pts',(20.2740212171349,-16.9053068980071,
11.7154922400669));
#147551=CARTESIAN_POINT('Ctrl Pts',(20.3403087741461,-16.9568993375336,
11.7196709181509));
#147552=CARTESIAN_POINT('Ctrl Pts',(20.4039685866081,-17.0116894785262,
11.7238495962348));
#147553=CARTESIAN_POINT('Ctrl Pts',(20.4687694554571,-17.0674616934192,
11.7281031741202));
#147554=CARTESIAN_POINT('Ctrl Pts',(20.5308470287296,-17.1265471378127,
11.7323567520057));
#147555=CARTESIAN_POINT('Ctrl Pts',(20.5898495933096,-17.1886445942429,
11.7366103298911));
#147556=CARTESIAN_POINT('Ctrl Pts',(20.647708278041,-17.2495381703069,11.7407814438691));
#147557=CARTESIAN_POINT('Ctrl Pts',(20.7026097887106,-17.3133276642815,
11.744952557847));
#147558=CARTESIAN_POINT('Ctrl Pts',(20.7542579245552,-17.3796902600722,
11.749123671825));
#147559=CARTESIAN_POINT('Ctrl Pts',(20.8058887293691,-17.446030587253,11.7532933861453));
#147560=CARTESIAN_POINT('Ctrl Pts',(20.8542680451848,-17.5149419387271,
11.7574631004657));
#147561=CARTESIAN_POINT('Ctrl Pts',(20.8991399066356,-17.5860683821311,
11.7616328147861));
#147562=CARTESIAN_POINT('Ctrl Pts',(20.944010171353,-17.6571922945511,11.7658023807301));
#147563=CARTESIAN_POINT('Ctrl Pts',(20.9853729851228,-17.7305307526506,
11.7699719466742));
#147564=CARTESIAN_POINT('Ctrl Pts',(21.0230164347473,-17.8056999688315,
11.7741415126182));
#147565=CARTESIAN_POINT('Ctrl Pts',(21.0619833816224,-17.8835120419222,
11.7784576753571));
#147566=CARTESIAN_POINT('Ctrl Pts',(21.0969643161937,-17.9632855357174,
11.7827738380961));
#147567=CARTESIAN_POINT('Ctrl Pts',(21.12777758528,-18.0445701833138,11.787090000835));
#147568=CARTESIAN_POINT('Ctrl Pts',(21.1575871153666,-18.1232069920642,
11.7912655650267));
#147569=CARTESIAN_POINT('Ctrl Pts',(21.1834962335158,-18.2032575521564,
11.7954411292184));
#147570=CARTESIAN_POINT('Ctrl Pts',(21.205391286958,-18.284298639549,11.79961669341));
#147571=CARTESIAN_POINT('Ctrl Pts',(21.228392207499,-18.369432919609,11.8040031554226));
#147572=CARTESIAN_POINT('Ctrl Pts',(21.2469627828282,-18.4556598489483,
11.8083896174351));
#147573=CARTESIAN_POINT('Ctrl Pts',(21.2610323380594,-18.5424788620813,
11.8127760794477));
#147574=CARTESIAN_POINT('Ctrl Pts',(21.2751018932905,-18.6292978752144,
11.8171625414602));
#147575=CARTESIAN_POINT('Ctrl Pts',(21.2846704408995,-18.7167083870925,
11.8215490034728));
#147576=CARTESIAN_POINT('Ctrl Pts',(21.2897303495758,-18.8042083214207,
11.8259354654853));
#147577=CARTESIAN_POINT('Ctrl Pts',(21.2945575272398,-18.8876836874037,
11.8301201717332));
#147578=CARTESIAN_POINT('Ctrl Pts',(21.2952996738552,-18.9715511471385,
11.834304877981));
#147579=CARTESIAN_POINT('Ctrl Pts',(21.2919118781324,-19.0553770947037,
11.8384895842288));
#147580=CARTESIAN_POINT('Ctrl Pts',(21.2885289204162,-19.1390833330158,
11.8426683144266));
#147581=CARTESIAN_POINT('Ctrl Pts',(21.2810277540022,-19.2227477211518,
11.8468470446243));
#147582=CARTESIAN_POINT('Ctrl Pts',(21.2694153767464,-19.3059334222111,
11.8510257748221));
#147583=CARTESIAN_POINT('Ctrl Pts',(21.2578166868028,-19.3890210736947,
11.8551995796214));
#147584=CARTESIAN_POINT('Ctrl Pts',(21.2421164820724,-19.4716307064917,
11.8593733844208));
#147585=CARTESIAN_POINT('Ctrl Pts',(21.2223736966772,-19.5533288166098,
11.8635471892201));
#147586=CARTESIAN_POINT('Ctrl Pts',(21.2026437041557,-19.6349739882196,
11.8677182894893));
#147587=CARTESIAN_POINT('Ctrl Pts',(21.1788764395496,-19.7157083639712,
11.8718893897585));
#147588=CARTESIAN_POINT('Ctrl Pts',(21.1511820426485,-19.7951079247032,
11.8760604900277));
#147589=CARTESIAN_POINT('Ctrl Pts',(21.1234972832818,-19.8744798547202,
11.8802301387714));
#147590=CARTESIAN_POINT('Ctrl Pts',(21.0918882575024,-19.9525174584111,
11.8843997875152));
#147591=CARTESIAN_POINT('Ctrl Pts',(21.0565147608215,-20.0288125118916,
11.8885694362589));
#147592=CARTESIAN_POINT('Ctrl Pts',(21.0211429628483,-20.1051039015276,
11.8927388847676));
#147593=CARTESIAN_POINT('Ctrl Pts',(20.9820072479426,-20.1796524905174,
11.8969083332763));
#147594=CARTESIAN_POINT('Ctrl Pts',(20.9393147224056,-20.2520719115269,
11.901077781785));
#147595=CARTESIAN_POINT('Ctrl Pts',(20.8965841485734,-20.3245558739396,
11.9052509461761));
#147596=CARTESIAN_POINT('Ctrl Pts',(20.8502906654462,-20.3949064803433,
11.9094241105673));
#147597=CARTESIAN_POINT('Ctrl Pts',(20.8006860848122,-20.4627642525701,
11.9135972749584));
#147598=CARTESIAN_POINT('Ctrl Pts',(20.7510600241141,-20.5306514089642,
11.9177722464375));
#147599=CARTESIAN_POINT('Ctrl Pts',(20.6981202983344,-20.5960432219192,
11.9219472179166));
#147600=CARTESIAN_POINT('Ctrl Pts',(20.6421591183141,-20.6586132482771,
11.9261221893957));
#147601=CARTESIAN_POINT('Ctrl Pts',(20.5861048295069,-20.7212873792883,
11.9303041072353));
#147602=CARTESIAN_POINT('Ctrl Pts',(20.5270193651334,-20.7811300141776,
11.9344860250748));
#147603=CARTESIAN_POINT('Ctrl Pts',(20.4652317777506,-20.8378516727745,
11.9386679429144));
#147604=CARTESIAN_POINT('Ctrl Pts',(20.4100681196037,-20.8884924942875,
11.9424015388658));
#147605=CARTESIAN_POINT('Ctrl Pts',(20.3527513118673,-20.9366460444125,
11.9461351348173));
#147606=CARTESIAN_POINT('Ctrl Pts',(20.2935357468249,-20.9821350335323,
11.9498687307687));
#147607=CARTESIAN_POINT('Ctrl Pts',(20.292281765808,-20.9805345212664,11.1497835179515));
#147608=CARTESIAN_POINT('Ctrl Pts',(20.0792747299441,-21.1470794377456,
11.1632078226604));
#147609=CARTESIAN_POINT('Ctrl Pts',(19.0902279379876,-21.7011259077543,
11.2190240629297));
#147610=CARTESIAN_POINT('Ctrl Pts',(16.9631832264668,-21.35816637253,11.3135258905595));
#147611=CARTESIAN_POINT('Ctrl Pts',(16.1754043811927,-19.7256331452917,
11.3946034134805));
#147612=CARTESIAN_POINT('Ctrl Pts',(16.1705865782758,-18.9507193134542,
11.433289000841));
#147613=CARTESIAN_POINT('',(16.1740004874608,-18.9535798097909,11.3667098902285));
#147614=CARTESIAN_POINT('Ctrl Pts',(20.2948050232963,-20.9838171774959,
11.0834063370138));
#147615=CARTESIAN_POINT('Ctrl Pts',(19.7177436700502,-21.4186341460381,
11.1194278873312));
#147616=CARTESIAN_POINT('Ctrl Pts',(18.0373628489283,-21.8291475591767,
11.1978413732092));
#147617=CARTESIAN_POINT('Ctrl Pts',(16.3822353344203,-20.4522479494082,
11.2922755723059));
#147618=CARTESIAN_POINT('Ctrl Pts',(16.1753927157401,-19.2766421922516,
11.350688221085));
#147619=CARTESIAN_POINT('Ctrl Pts',(16.177204683354,-18.953597107844,11.3667089343037));
#147620=CARTESIAN_POINT('Ctrl Pts',(16.1740004874608,-18.9535798097909,
11.3667098902285));
#147621=CARTESIAN_POINT('Ctrl Pts',(16.1739481146197,-18.8687123476393,
11.3709134538372));
#147622=CARTESIAN_POINT('Ctrl Pts',(16.1781202862138,-18.7838299700766,
11.3751170174459));
#147623=CARTESIAN_POINT('Ctrl Pts',(16.1864949217896,-18.699377996817,11.3793205810546));
#147624=CARTESIAN_POINT('Ctrl Pts',(16.1948707822013,-18.6149136719983,
11.3835247594573));
#147625=CARTESIAN_POINT('Ctrl Pts',(16.2074502833288,-18.5308803238368,
11.3877289378599));
#147626=CARTESIAN_POINT('Ctrl Pts',(16.2241595327126,-18.447717510946,11.3919331162626));
#147627=CARTESIAN_POINT('Ctrl Pts',(16.2408759290274,-18.3645191274036,
11.3961390928892));
#147628=CARTESIAN_POINT('Ctrl Pts',(16.2617254950327,-18.2821924593937,
11.4003450695159));
#147629=CARTESIAN_POINT('Ctrl Pts',(16.2865836343726,-18.2011650425965,
11.4045510461425));
#147630=CARTESIAN_POINT('Ctrl Pts',(16.3114761780105,-18.1200254817903,
11.408762843948));
#147631=CARTESIAN_POINT('Ctrl Pts',(16.3403882340966,-18.0401891906195,
11.4129746417534));
#147632=CARTESIAN_POINT('Ctrl Pts',(16.3731460171586,-17.9620664306621,
11.4171864395589));
#147633=CARTESIAN_POINT('Ctrl Pts',(16.4059305542806,-17.8838798659902,
11.4214016772397));
#147634=CARTESIAN_POINT('Ctrl Pts',(16.4425668768385,-17.8074100228066,
11.4256169149205));
#147635=CARTESIAN_POINT('Ctrl Pts',(16.4828349986458,-17.7330430127859,
11.4298321526013));
#147636=CARTESIAN_POINT('Ctrl Pts',(16.5231739006091,-17.6585452862497,
11.4340547994973));
#147637=CARTESIAN_POINT('Ctrl Pts',(16.5671571084147,-17.5861581518398,
11.4382774463933));
#147638=CARTESIAN_POINT('Ctrl Pts',(16.6145212917447,-17.5162388759782,
11.4425000932893));
#147639=CARTESIAN_POINT('Ctrl Pts',(16.6269438222717,-17.4979006660113,
11.4436075959693));
#147640=CARTESIAN_POINT('Ctrl Pts',(16.6395987151329,-17.4797320374711,
11.4447150986492));
#147641=CARTESIAN_POINT('Ctrl Pts',(16.6524807786036,-17.4617390393098,
11.4458226013291));
#147642=CARTESIAN_POINT('Ctrl Pts',(16.7011549053849,-17.3937535433782,
11.4500072357222));
#147643=CARTESIAN_POINT('Ctrl Pts',(16.7532538754926,-17.3280286903787,
11.4541918701152));
#147644=CARTESIAN_POINT('Ctrl Pts',(16.8085402991528,-17.2649300724589,
11.4583765045082));
#147645=CARTESIAN_POINT('Ctrl Pts',(16.8637480294321,-17.2019212676117,
11.4625551825922));
#147646=CARTESIAN_POINT('Ctrl Pts',(16.9221339008884,-17.1415316158069,
11.4667338606761));
#147647=CARTESIAN_POINT('Ctrl Pts',(16.9834181011141,-17.0840966258147,
11.4709125387601));
#147648=CARTESIAN_POINT('Ctrl Pts',(17.0458007765846,-17.0256321549047,
11.4751661166455));
#147649=CARTESIAN_POINT('Ctrl Pts',(17.1111864272472,-16.9702297043271,
11.479419694531));
#147650=CARTESIAN_POINT('Ctrl Pts',(17.1792379481546,-16.9182067553113,
11.4836732724164));
#147651=CARTESIAN_POINT('Ctrl Pts',(17.2459701575375,-16.8671923726766,
11.4878443863943));
#147652=CARTESIAN_POINT('Ctrl Pts',(17.3152654110889,-16.8194279167438,
11.4920155003723));
#147653=CARTESIAN_POINT('Ctrl Pts',(17.3867710660549,-16.7751733648402,
11.4961866143502));
#147654=CARTESIAN_POINT('Ctrl Pts',(17.4582527266079,-16.7309336629788,
11.5003563286706));
#147655=CARTESIAN_POINT('Ctrl Pts',(17.5319429246537,-16.6902017679485,
11.504526042991));
#147656=CARTESIAN_POINT('Ctrl Pts',(17.6074603942083,-16.6531941107213,
11.5086957573114));
#147657=CARTESIAN_POINT('Ctrl Pts',(17.6829751765273,-16.6161877703852,
11.5128653232554));
#147658=CARTESIAN_POINT('Ctrl Pts',(17.7603166876031,-16.5829056060341,
11.5170348891995));
#147659=CARTESIAN_POINT('Ctrl Pts',(17.8390806772786,-16.5535172700601,
11.5212044551435));
#147660=CARTESIAN_POINT('Ctrl Pts',(17.9206139116649,-16.5230956764478,
11.5255206178824));
#147661=CARTESIAN_POINT('Ctrl Pts',(18.0036710203273,-16.4968470041692,
11.5298367806213));
#147662=CARTESIAN_POINT('Ctrl Pts',(18.0877848913439,-16.4749037093111,
11.5341529433603));
#147663=CARTESIAN_POINT('Ctrl Pts',(18.1691587618594,-16.453675214975,11.5383285075519));
#147664=CARTESIAN_POINT('Ctrl Pts',(18.2515211332009,-16.4364759603011,
11.5425040717436));
#147665=CARTESIAN_POINT('Ctrl Pts',(18.3344390537292,-16.4233736831601,
11.5466796359353));
#147666=CARTESIAN_POINT('Ctrl Pts',(18.4215449613047,-16.4096096411485,
11.5510660979478));
#147667=CARTESIAN_POINT('Ctrl Pts',(18.5092634338796,-16.4003673913993,
11.5554525599604));
#147668=CARTESIAN_POINT('Ctrl Pts',(18.5970892183629,-16.3956636688668,
11.5598390219729));
#147669=CARTESIAN_POINT('Ctrl Pts',(18.6849150028461,-16.3909599463343,
11.5642254839854));
#147670=CARTESIAN_POINT('Ctrl Pts',(18.7728475188788,-16.3907946760441,
11.568611945998));
#147671=CARTESIAN_POINT('Ctrl Pts',(18.8603867536229,-16.3951217493771,
11.5729984080105));
#147672=CARTESIAN_POINT('Ctrl Pts',(18.9438981784123,-16.3992497276517,
11.5771830424036));
#147673=CARTESIAN_POINT('Ctrl Pts',(19.0273625629856,-16.4074811003133,
11.5813676767966));
#147674=CARTESIAN_POINT('Ctrl Pts',(19.1103440076207,-16.4198141482253,
11.5855523111897));
#147675=CARTESIAN_POINT('Ctrl Pts',(19.1932073384403,-16.4321296415701,
11.5897309892736));
#147676=CARTESIAN_POINT('Ctrl Pts',(19.2755886435822,-16.4485351465588,
11.5939096673576));
#147677=CARTESIAN_POINT('Ctrl Pts',(19.3570543561167,-16.4689769897715,
11.5980883454415));
#147678=CARTESIAN_POINT('Ctrl Pts',(19.4399802830001,-16.4897852383326,
11.6023419233269));
#147679=CARTESIAN_POINT('Ctrl Pts',(19.5219569888747,-16.5147759273293,
11.6065955012124));
#147680=CARTESIAN_POINT('Ctrl Pts',(19.6025350537547,-16.5438374514167,
11.6108490790978));
#147681=CARTESIAN_POINT('Ctrl Pts',(19.681550955612,-16.5723355611508,11.6150201930758));
#147682=CARTESIAN_POINT('Ctrl Pts',(19.7592215106215,-16.6047479091041,
11.6191913070537));
#147683=CARTESIAN_POINT('Ctrl Pts',(19.8351372401589,-16.6409186993238,
11.6233624210317));
#147684=CARTESIAN_POINT('Ctrl Pts',(19.9110274954401,-16.6770773520855,
11.627532135352));
#147685=CARTESIAN_POINT('Ctrl Pts',(19.9851636797555,-16.716991744677,11.6317018496724));
#147686=CARTESIAN_POINT('Ctrl Pts',(20.0571574368627,-16.7604584427223,
11.6358715639928));
#147687=CARTESIAN_POINT('Ctrl Pts',(20.129148632123,-16.803923594036,11.6400411299368));
#147688=CARTESIAN_POINT('Ctrl Pts',(20.198997158373,-16.8509405609741,11.6442106958809));
#147689=CARTESIAN_POINT('Ctrl Pts',(20.2663415518561,-16.9012612627506,
11.6483802618249));
#147690=CARTESIAN_POINT('Ctrl Pts',(20.3360536911358,-16.9533511783243,
11.6526964245638));
#147691=CARTESIAN_POINT('Ctrl Pts',(20.403081908196,-17.008981154178,11.6570125873028));
#147692=CARTESIAN_POINT('Ctrl Pts',(20.4670619896056,-17.0678301190751,
11.6613287500417));
#147693=CARTESIAN_POINT('Ctrl Pts',(20.5289579265927,-17.1247620851305,
11.6655043142334));
#147694=CARTESIAN_POINT('Ctrl Pts',(20.5880009674137,-17.1847061749556,
11.6696798784251));
#147695=CARTESIAN_POINT('Ctrl Pts',(20.6438998067281,-17.2473350099624,
11.6738554426167));
#147696=CARTESIAN_POINT('Ctrl Pts',(20.7026219635295,-17.3131270785395,
11.6782419046293));
#147697=CARTESIAN_POINT('Ctrl Pts',(20.7578735784432,-17.3818817777297,
11.6826283666418));
#147698=CARTESIAN_POINT('Ctrl Pts',(20.809367096106,-17.4531833279548,11.6870148286544));
#147699=CARTESIAN_POINT('Ctrl Pts',(20.8608606137687,-17.5244848781798,
11.6914012906669));
#147700=CARTESIAN_POINT('Ctrl Pts',(20.9085957830846,-17.5983327508675,
11.6957877526794));
#147701=CARTESIAN_POINT('Ctrl Pts',(20.9523407266399,-17.6742815566288,
11.700174214692));
#147702=CARTESIAN_POINT('Ctrl Pts',(20.9940729004966,-17.746735845254,11.704358849085));
#147703=CARTESIAN_POINT('Ctrl Pts',(21.0323293070736,-17.8213716700563,
11.7085434834781));
#147704=CARTESIAN_POINT('Ctrl Pts',(21.0668754476401,-17.8978215778161,
11.7127281178711));
#147705=CARTESIAN_POINT('Ctrl Pts',(21.1013724160514,-17.9741626685948,
11.7169067959551));
#147706=CARTESIAN_POINT('Ctrl Pts',(21.1321694205717,-18.0523122977901,
11.721085474039));
#147707=CARTESIAN_POINT('Ctrl Pts',(21.159076910497,-18.131876851824,11.725264152123));
#147708=CARTESIAN_POINT('Ctrl Pts',(21.1864666978413,-18.2128675433069,
11.7295177300084));
#147709=CARTESIAN_POINT('Ctrl Pts',(21.2098259193361,-18.2953239658205,
11.7337713078938));
#147710=CARTESIAN_POINT('Ctrl Pts',(21.2290051549002,-18.3788078184225,
11.7380248857793));
#147711=CARTESIAN_POINT('Ctrl Pts',(21.2478125635577,-18.4606731736366,
11.7421959997572));
#147712=CARTESIAN_POINT('Ctrl Pts',(21.2626005065823,-18.5435260079661,
11.7463671137352));
#147713=CARTESIAN_POINT('Ctrl Pts',(21.2732783407021,-18.6269376852951,
11.7505382277131));
#147714=CARTESIAN_POINT('Ctrl Pts',(21.2839525917715,-18.7103213730302,
11.7547079420335));
#147715=CARTESIAN_POINT('Ctrl Pts',(21.2905194146576,-18.7942630754074,
11.7588776563539));
#147716=CARTESIAN_POINT('Ctrl Pts',(21.2929396556081,-18.8783261311164,
11.7630473706743));
#147717=CARTESIAN_POINT('Ctrl Pts',(21.295359810436,-18.9623861955009,11.7672169366183));
#147718=CARTESIAN_POINT('Ctrl Pts',(21.2936336643145,-19.0465671447645,
11.7713865025623));
#147719=CARTESIAN_POINT('Ctrl Pts',(21.2877741604491,-19.1304307636664,
11.7755560685064));
#147720=CARTESIAN_POINT('Ctrl Pts',(21.2817086436563,-19.2172429239521,
11.7798722312453));
#147721=CARTESIAN_POINT('Ctrl Pts',(21.2712137402018,-19.3037144978781,
11.7841883939842));
#147722=CARTESIAN_POINT('Ctrl Pts',(21.2563622783627,-19.389365449816,11.7885045567231));
#147723=CARTESIAN_POINT('Ctrl Pts',(21.2419946013309,-19.4722263310034,
11.7926801209148));
#147724=CARTESIAN_POINT('Ctrl Pts',(21.2235499863025,-19.5543187834628,
11.7968556851065));
#147725=CARTESIAN_POINT('Ctrl Pts',(21.2011460288054,-19.6352206616825,
11.8010312492982));
#147726=CARTESIAN_POINT('Ctrl Pts',(21.1776105006754,-19.7202087014452,
11.8054177113107));
#147727=CARTESIAN_POINT('Ctrl Pts',(21.1497053305465,-19.8038821804657,
11.8098041733232));
#147728=CARTESIAN_POINT('Ctrl Pts',(21.1176244749812,-19.8857742565901,
11.8141906353358));
#147729=CARTESIAN_POINT('Ctrl Pts',(21.085543619416,-19.9676663327146,11.8185770973483));
#147730=CARTESIAN_POINT('Ctrl Pts',(21.0492873869465,-20.0477765087051,
11.8229635593609));
#147731=CARTESIAN_POINT('Ctrl Pts',(21.0091047687183,-20.1256687315232,
11.8273500213734));
#147732=CARTESIAN_POINT('Ctrl Pts',(20.9707678090114,-20.1999832271766,
11.8315350054497));
#147733=CARTESIAN_POINT('Ctrl Pts',(20.9287145340163,-20.2725556853794,
11.8357199895261));
#147734=CARTESIAN_POINT('Ctrl Pts',(20.8831270316855,-20.3429899358654,
11.8399049736024));
#147735=CARTESIAN_POINT('Ctrl Pts',(20.837615826569,-20.4133063045453,11.8440829535085));
#147736=CARTESIAN_POINT('Ctrl Pts',(20.7885824023179,-20.4814911976132,
11.8482609334146));
#147737=CARTESIAN_POINT('Ctrl Pts',(20.7362550110441,-20.5471723639622,
11.8524389133207));
#147738=CARTESIAN_POINT('Ctrl Pts',(20.6839782703651,-20.6127899538542,
11.8566128491275));
#147739=CARTESIAN_POINT('Ctrl Pts',(20.6284141773795,-20.6759082704892,
11.8607867849342));
#147740=CARTESIAN_POINT('Ctrl Pts',(20.5698341380259,-20.736184132218,11.864960720741));
#147741=CARTESIAN_POINT('Ctrl Pts',(20.5112960173948,-20.7964168617272,
11.8691316697615));
#147742=CARTESIAN_POINT('Ctrl Pts',(20.4497465580618,-20.8538108487051,
11.873302618782));
#147743=CARTESIAN_POINT('Ctrl Pts',(20.3854963550761,-20.9080572049842,
11.8774735678025));
#147744=CARTESIAN_POINT('Ctrl Pts',(20.3554224770341,-20.9334485380407,
11.8794258824464));
#147745=CARTESIAN_POINT('Ctrl Pts',(20.3247574231983,-20.9581507568336,
11.8813781970903));
#147746=CARTESIAN_POINT('Ctrl Pts',(20.2935357468249,-20.9821350335323,
11.8833305117342));
#147747=CARTESIAN_POINT('Origin',(18.734,-18.952,-1.76670989022851));
#147748=CARTESIAN_POINT('',(20.2935357468249,-20.9821350335323,12.7499597608822));
#147749=CARTESIAN_POINT('',(20.2929505273092,-20.9813917755493,12.683192392576));
#147750=CARTESIAN_POINT('',(20.2935357468249,-20.9821350335323,-1.76670989022851));
#147751=CARTESIAN_POINT('',(16.1740010233873,-18.9542890482673,12.2332901098107));
#147752=CARTESIAN_POINT('Ctrl Pts',(16.1740010233873,-18.9542890482673,
12.2332901098107));
#147753=CARTESIAN_POINT('Ctrl Pts',(16.1739252094451,-18.869501140071,12.2375129674107));
#147754=CARTESIAN_POINT('Ctrl Pts',(16.1780663695147,-18.7845778436852,
12.2417358250107));
#147755=CARTESIAN_POINT('Ctrl Pts',(16.1864353355331,-18.6999796032861,
12.2459586826108));
#147756=CARTESIAN_POINT('Ctrl Pts',(16.1945865434513,-18.6175825848873,
12.2500716626647));
#147757=CARTESIAN_POINT('Ctrl Pts',(16.2067481850333,-18.5354944186516,
12.2541846427187));
#147758=CARTESIAN_POINT('Ctrl Pts',(16.2228775801224,-18.4541403888766,
12.2582976227727));
#147759=CARTESIAN_POINT('Ctrl Pts',(16.2389992540557,-18.3728253033474,
12.2624086339395));
#147760=CARTESIAN_POINT('Ctrl Pts',(16.2590848209399,-18.2922441216164,
12.2665196451063));
#147761=CARTESIAN_POINT('Ctrl Pts',(16.2830401055299,-18.2128142346481,
12.2706306562731));
#147762=CARTESIAN_POINT('Ctrl Pts',(16.3069915898917,-18.13339694831,12.2747410152756));
#147763=CARTESIAN_POINT('Ctrl Pts',(16.3348114354692,-18.0551310480635,
12.2788513742782));
#147764=CARTESIAN_POINT('Ctrl Pts',(16.3663553936721,-17.9784194855451,
12.2829617332808));
#147765=CARTESIAN_POINT('Ctrl Pts',(16.3994039228382,-17.8980489659369,
12.2872681465249));
#147766=CARTESIAN_POINT('Ctrl Pts',(16.4365404963283,-17.8193852938553,
12.2915745597691));
#147767=CARTESIAN_POINT('Ctrl Pts',(16.4775431085385,-17.74286713014,12.2958809730133));
#147768=CARTESIAN_POINT('Ctrl Pts',(16.5167281737212,-17.6697408322964,
12.2999964933322));
#147769=CARTESIAN_POINT('Ctrl Pts',(16.5594435017452,-17.5985742591835,
12.304112013651));
#147770=CARTESIAN_POINT('Ctrl Pts',(16.6054498638679,-17.5297221375653,
12.3082275339699));
#147771=CARTESIAN_POINT('Ctrl Pts',(16.6514869443888,-17.46082404346,12.3123458022172));
#147772=CARTESIAN_POINT('Ctrl Pts',(16.7008191449124,-17.394243852655,12.3164640704645));
#147773=CARTESIAN_POINT('Ctrl Pts',(16.7531665958489,-17.3303036582026,
12.3205823387118));
#147774=CARTESIAN_POINT('Ctrl Pts',(16.8055945346489,-17.2662651512335,
12.3247069390843));
#147775=CARTESIAN_POINT('Ctrl Pts',(16.8610466479906,-17.204875081261,12.3288315394568));
#147776=CARTESIAN_POINT('Ctrl Pts',(16.9192065009782,-17.1464184992341,
12.3329561398293));
#147777=CARTESIAN_POINT('Ctrl Pts',(16.9271149034353,-17.1384697484517,
12.3335169906232));
#147778=CARTESIAN_POINT('Ctrl Pts',(16.9350733229401,-17.1305751748483,
12.3340778414171));
#147779=CARTESIAN_POINT('Ctrl Pts',(16.9430809195059,-17.122735435449,12.334638692211));
#147780=CARTESIAN_POINT('Ctrl Pts',(17.0028274053095,-17.0642413698601,
12.338823326604));
#147781=CARTESIAN_POINT('Ctrl Pts',(17.0655538444184,-17.0085686402269,
12.3430079609971));
#147782=CARTESIAN_POINT('Ctrl Pts',(17.1309629349575,-16.9560360303603,
12.3471925953901));
#147783=CARTESIAN_POINT('Ctrl Pts',(17.1962789237522,-16.9035781941616,
12.3513712734741));
#147784=CARTESIAN_POINT('Ctrl Pts',(17.2642696237811,-16.8542518853561,
12.355549951558));
#147785=CARTESIAN_POINT('Ctrl Pts',(17.33460118292,-16.8083388908796,12.359728629642));
#147786=CARTESIAN_POINT('Ctrl Pts',(17.4061933847101,-16.7616029389743,
12.3639822075274));
#147787=CARTESIAN_POINT('Ctrl Pts',(17.4802108463248,-16.7184042096099,
12.3682357854128));
#147788=CARTESIAN_POINT('Ctrl Pts',(17.5562664269219,-16.6789967816027,
12.3724893632983));
#147789=CARTESIAN_POINT('Ctrl Pts',(17.6308475216787,-16.6403533434847,
12.3766604772762));
#147790=CARTESIAN_POINT('Ctrl Pts',(17.7073879875333,-16.6053557363939,
12.3808315912542));
#147791=CARTESIAN_POINT('Ctrl Pts',(17.7854953736987,-16.5741987101768,
12.3850027052321));
#147792=CARTESIAN_POINT('Ctrl Pts',(17.8635765501766,-16.5430521390006,
12.3891724195525));
#147793=CARTESIAN_POINT('Ctrl Pts',(17.9432231757915,-16.5157437595367,
12.3933421338729));
#147794=CARTESIAN_POINT('Ctrl Pts',(18.0240221782535,-16.4924204642606,
12.3975118481932));
#147795=CARTESIAN_POINT('Ctrl Pts',(18.1048183055401,-16.4690979989274,
12.4016814141373));
#147796=CARTESIAN_POINT('Ctrl Pts',(18.1867662859185,-16.4497604625989,
12.4058509800813));
#147797=CARTESIAN_POINT('Ctrl Pts',(18.2694385404883,-16.4345046871272,
12.4100205460254));
#147798=CARTESIAN_POINT('Ctrl Pts',(18.3550174495415,-16.4187125374101,
12.4143367087643));
#147799=CARTESIAN_POINT('Ctrl Pts',(18.4413719926989,-16.4072946141391,
12.4186528715032));
#147800=CARTESIAN_POINT('Ctrl Pts',(18.5280191484749,-16.400300196182,12.4229690342421));
#147801=CARTESIAN_POINT('Ctrl Pts',(18.6118437822652,-16.3935336206541,
12.4271445984338));
#147802=CARTESIAN_POINT('Ctrl Pts',(18.6959417854335,-16.3909067522804,
12.4313201626255));
#147803=CARTESIAN_POINT('Ctrl Pts',(18.7798750222016,-16.3924110716097,
12.4354957268172));
#147804=CARTESIAN_POINT('Ctrl Pts',(18.8680475272266,-16.3939913705322,
12.4398821888297));
#147805=CARTESIAN_POINT('Ctrl Pts',(18.9560376012526,-16.4001311167978,
12.4442686508422));
#147806=CARTESIAN_POINT('Ctrl Pts',(19.0433447687656,-16.4107590011891,
12.4486551128548));
#147807=CARTESIAN_POINT('Ctrl Pts',(19.1306519362786,-16.4213868855804,
12.4530415748673));
#147808=CARTESIAN_POINT('Ctrl Pts',(19.2172756387743,-16.4365027334242,
12.4574280368799));
#147809=CARTESIAN_POINT('Ctrl Pts',(19.3027314805895,-16.4559742583486,
12.4618144988924));
#147810=CARTESIAN_POINT('Ctrl Pts',(19.3842553724469,-16.4745498695475,
12.4659991332855));
#147811=CARTESIAN_POINT('Ctrl Pts',(19.4650199594566,-16.4971582855303,
12.4701837676785));
#147812=CARTESIAN_POINT('Ctrl Pts',(19.5445962710158,-16.5237220740996,
12.4743684020716));
#147813=CARTESIAN_POINT('Ctrl Pts',(19.6240593155451,-16.5502480524038,
12.4785470801555));
#147814=CARTESIAN_POINT('Ctrl Pts',(19.702337011573,-16.5807180759575,12.4827257582394));
#147815=CARTESIAN_POINT('Ctrl Pts',(19.7790117130572,-16.6150039538815,
12.4869044363234));
#147816=CARTESIAN_POINT('Ctrl Pts',(19.8570607534603,-16.6499043815265,
12.4911580142088));
#147817=CARTESIAN_POINT('Ctrl Pts',(19.9334482966285,-16.6887587003509,
12.4954115920943));
#147818=CARTESIAN_POINT('Ctrl Pts',(20.0077511504909,-16.7313789142172,
12.4996651699797));
#147819=CARTESIAN_POINT('Ctrl Pts',(20.0806134985411,-16.7731728520712,
12.5038362839577));
#147820=CARTESIAN_POINT('Ctrl Pts',(20.1514708500755,-16.8185877301275,
12.5080073979356));
#147821=CARTESIAN_POINT('Ctrl Pts',(20.2199470251256,-16.8673989737793,
12.5121785119136));
#147822=CARTESIAN_POINT('Ctrl Pts',(20.2884002223337,-16.9161938383468,
12.5163482262339));
#147823=CARTESIAN_POINT('Ctrl Pts',(20.3544734556457,-16.9683825382778,
12.5205179405543));
#147824=CARTESIAN_POINT('Ctrl Pts',(20.4178196235398,-17.0236972552572,
12.5246876548747));
#147825=CARTESIAN_POINT('Ctrl Pts',(20.4811635373054,-17.0790100039017,
12.5288572208188));
#147826=CARTESIAN_POINT('Ctrl Pts',(20.5417802326388,-17.1374482452018,
12.5330267867628));
#147827=CARTESIAN_POINT('Ctrl Pts',(20.5993568489269,-17.198704866213,12.5371963527068));
#147828=CARTESIAN_POINT('Ctrl Pts',(20.6589577880153,-17.2621151944506,
12.5415125154458));
#147829=CARTESIAN_POINT('Ctrl Pts',(20.7153005309283,-17.3285453940347,
12.5458286781847));
#147830=CARTESIAN_POINT('Ctrl Pts',(20.7680821915678,-17.3976159940521,
12.5501448409236));
#147831=CARTESIAN_POINT('Ctrl Pts',(20.8191444951638,-17.464436626539,12.5543204051153));
#147832=CARTESIAN_POINT('Ctrl Pts',(20.8668739298254,-17.5337278643778,
12.558495969307));
#147833=CARTESIAN_POINT('Ctrl Pts',(20.9110405044759,-17.6051166932985,
12.5626715334987));
#147834=CARTESIAN_POINT('Ctrl Pts',(20.957437827816,-17.680111202257,12.5670579955112));
#147835=CARTESIAN_POINT('Ctrl Pts',(20.999902631049,-17.7574202579858,12.5714444575237));
#147836=CARTESIAN_POINT('Ctrl Pts',(21.0382239760384,-17.8365844414525,
12.5758309195363));
#147837=CARTESIAN_POINT('Ctrl Pts',(21.0765453210278,-17.9157486249193,
12.5802173815488));
#147838=CARTESIAN_POINT('Ctrl Pts',(21.1107230523385,-17.9967673719632,
12.5846038435614));
#147839=CARTESIAN_POINT('Ctrl Pts',(21.1406062076889,-18.0791617783844,
12.5889903055739));
#147840=CARTESIAN_POINT('Ctrl Pts',(21.1691143947643,-18.1577650960285,
12.5931749399669));
#147841=CARTESIAN_POINT('Ctrl Pts',(21.193820633909,-18.2379128391996,12.59735957436));
#147842=CARTESIAN_POINT('Ctrl Pts',(21.2145578396958,-18.3192023989271,
12.601544208753));
#147843=CARTESIAN_POINT('Ctrl Pts',(21.2352655286369,-18.4003762530279,
12.605722886837));
#147844=CARTESIAN_POINT('Ctrl Pts',(21.25201529302,-18.4826882535134,12.6099015649209));
#147845=CARTESIAN_POINT('Ctrl Pts',(21.2646888572063,-18.5657178388641,
12.6140802430049));
#147846=CARTESIAN_POINT('Ctrl Pts',(21.2775895859224,-18.65023566986,12.6183338208903));
#147847=CARTESIAN_POINT('Ctrl Pts',(21.2862663809329,-18.7354966109228,
12.6225873987757));
#147848=CARTESIAN_POINT('Ctrl Pts',(21.2906482513971,-18.8210430657491,
12.6268409766612));
#147849=CARTESIAN_POINT('Ctrl Pts',(21.2949451707518,-18.9049310356184,
12.6310120906391));
#147850=CARTESIAN_POINT('Ctrl Pts',(21.2951121858363,-18.9890930669704,
12.6351832046171));
#147851=CARTESIAN_POINT('Ctrl Pts',(21.2911345092731,-19.0730912940082,
12.639354318595));
#147852=CARTESIAN_POINT('Ctrl Pts',(21.2871581674577,-19.1570613346296,
12.6435240329154));
#147853=CARTESIAN_POINT('Ctrl Pts',(21.2790399178703,-19.2408672209647,
12.6476937472358));
#147854=CARTESIAN_POINT('Ctrl Pts',(21.2668170738604,-19.3240721305896,
12.6518634615562));
#147855=CARTESIAN_POINT('Ctrl Pts',(21.2545946647916,-19.4072740794267,
12.6560330275002));
#147856=CARTESIAN_POINT('Ctrl Pts',(21.2382680194079,-19.4898746390487,
12.6602025934442));
#147857=CARTESIAN_POINT('Ctrl Pts',(21.2179260255778,-19.5714445087795,
12.6643721593883));
#147858=CARTESIAN_POINT('Ctrl Pts',(21.1968688323393,-19.6558822745029,
12.6686883221272));
#147859=CARTESIAN_POINT('Ctrl Pts',(21.1715088054102,-19.7392150119469,
12.6730044848661));
#147860=CARTESIAN_POINT('Ctrl Pts',(21.1420010732758,-19.8209826414278,
12.6773206476051));
#147861=CARTESIAN_POINT('Ctrl Pts',(21.113454552412,-19.9000866989788,12.6814962117967));
#147862=CARTESIAN_POINT('Ctrl Pts',(21.0810266246877,-19.9777256330122,
12.6856717759884));
#147863=CARTESIAN_POINT('Ctrl Pts',(21.0449064462655,-20.0535041518799,
12.6898473401801));
#147864=CARTESIAN_POINT('Ctrl Pts',(21.0069619234988,-20.1331100635892,
12.6942338021926));
#147865=CARTESIAN_POINT('Ctrl Pts',(20.9649426346355,-20.2106621684913,
12.6986202642052));
#147866=CARTESIAN_POINT('Ctrl Pts',(20.9191207015645,-20.2857344261862,
12.7030067262177));
#147867=CARTESIAN_POINT('Ctrl Pts',(20.8732987684935,-20.3608066838811,
12.7073931882303));
#147868=CARTESIAN_POINT('Ctrl Pts',(20.8236745814507,-20.433398658303,12.7117796502428));
#147869=CARTESIAN_POINT('Ctrl Pts',(20.7705691100602,-20.5031241923033,
12.7161661122553));
#147870=CARTESIAN_POINT('Ctrl Pts',(20.7199091712282,-20.5696388318498,
12.7203505755776));
#147871=CARTESIAN_POINT('Ctrl Pts',(20.6658929673645,-20.6337927963153,
12.7245350388999));
#147872=CARTESIAN_POINT('Ctrl Pts',(20.6087685573973,-20.6952277120889,
12.7287195022221));
#147873=CARTESIAN_POINT('Ctrl Pts',(20.5517322346214,-20.7565678937692,
12.7328975130029));
#147874=CARTESIAN_POINT('Ctrl Pts',(20.4915975412145,-20.815197025317,12.7370755237838));
#147875=CARTESIAN_POINT('Ctrl Pts',(20.4286539389059,-20.8707881663567,
12.7412535345646));
#147876=CARTESIAN_POINT('Ctrl Pts',(20.3849328735721,-20.9094021607936,
12.7441556100038));
#147877=CARTESIAN_POINT('Ctrl Pts',(20.3398574638174,-20.9465510096566,
12.747057685443));
#147878=CARTESIAN_POINT('Ctrl Pts',(20.2935357468249,-20.9821350335323,
12.7499597608822));
#147879=CARTESIAN_POINT('Ctrl Pts',(20.2935357468249,-20.9821350335323,
11.9498687307687));
#147880=CARTESIAN_POINT('Ctrl Pts',(20.2763932990299,-20.9953037438313,
11.9509495779013));
#147881=CARTESIAN_POINT('Ctrl Pts',(20.2590918338935,-21.0082493295476,
11.952030425034));
#147882=CARTESIAN_POINT('Ctrl Pts',(20.2416377781119,-21.0209679383717,
11.9531112721667));
#147883=CARTESIAN_POINT('Ctrl Pts',(20.1740622256448,-21.0702096177069,
11.9572959065597));
#147884=CARTESIAN_POINT('Ctrl Pts',(20.1039459219093,-21.1162287760929,
11.9614805409527));
#147885=CARTESIAN_POINT('Ctrl Pts',(20.0316291334116,-21.1587529612808,
11.9656651753458));
#147886=CARTESIAN_POINT('Ctrl Pts',(19.9594152789112,-21.2012166185545,
11.9698438534297));
#147887=CARTESIAN_POINT('Ctrl Pts',(19.8850075541825,-21.2401949526838,
11.9740225315137));
#147888=CARTESIAN_POINT('Ctrl Pts',(19.8087770431608,-21.2754574038476,
11.9782012095976));
#147889=CARTESIAN_POINT('Ctrl Pts',(19.731180155015,-21.311351909106,11.9824547874831));
#147890=CARTESIAN_POINT('Ctrl Pts',(19.6516948805992,-21.343395722762,11.9867083653685));
#147891=CARTESIAN_POINT('Ctrl Pts',(19.5707410268107,-21.3713934062181,
11.9909619432539));
#147892=CARTESIAN_POINT('Ctrl Pts',(19.4913566214465,-21.3988482999475,
11.9951330572319));
#147893=CARTESIAN_POINT('Ctrl Pts',(19.4105605259062,-21.4224123904405,
11.9993041712098));
#147894=CARTESIAN_POINT('Ctrl Pts',(19.3287692237674,-21.4419497124358,
12.0034752851878));
#147895=CARTESIAN_POINT('Ctrl Pts',(19.24700536749,-21.461480478494,12.0076449995082));
#147896=CARTESIAN_POINT('Ctrl Pts',(19.1642474149188,-21.4769870528098,
12.0118147138285));
#147897=CARTESIAN_POINT('Ctrl Pts',(19.0809253355101,-21.4883838060477,
12.0159844281489));
#147898=CARTESIAN_POINT('Ctrl Pts',(18.9976062210584,-21.4997801537403,
12.0201539940929));
#147899=CARTESIAN_POINT('Ctrl Pts',(18.9137234755861,-21.5070669096296,
12.024323560037));
#147900=CARTESIAN_POINT('Ctrl Pts',(18.8297141852437,-21.5102100763509,
12.028493125981));
#147901=CARTESIAN_POINT('Ctrl Pts',(18.7427512318893,-21.5134637529366,
12.0328092887199));
#147902=CARTESIAN_POINT('Ctrl Pts',(18.6556531965172,-21.5122770220956,
12.0371254514589));
#147903=CARTESIAN_POINT('Ctrl Pts',(18.5689051504098,-21.5066709554537,
12.0414416141978));
#147904=CARTESIAN_POINT('Ctrl Pts',(18.4849829127801,-21.501247505843,12.0456171783895));
#147905=CARTESIAN_POINT('Ctrl Pts',(18.4013886754049,-21.4916883190585,
12.0497927425811));
#147906=CARTESIAN_POINT('Ctrl Pts',(18.3185547392504,-21.4780651684627,
12.0539683067728));
#147907=CARTESIAN_POINT('Ctrl Pts',(18.2315370578995,-21.4637539449163,
12.0583547687854));
#147908=CARTESIAN_POINT('Ctrl Pts',(18.1453590723583,-21.444957551129,12.0627412307979));
#147909=CARTESIAN_POINT('Ctrl Pts',(18.0605056905582,-21.4218189033104,
12.0671276928105));
#147910=CARTESIAN_POINT('Ctrl Pts',(17.975652308758,-21.3986802554919,12.071514154823));
#147911=CARTESIAN_POINT('Ctrl Pts',(17.8921240580818,-21.371199607226,12.0759006168356));
#147912=CARTESIAN_POINT('Ctrl Pts',(17.8103811197836,-21.3395778865008,
12.0802870788481));
#147913=CARTESIAN_POINT('Ctrl Pts',(17.7323992952486,-21.3094111280208,
12.0844717132412));
#147914=CARTESIAN_POINT('Ctrl Pts',(17.6557518403844,-21.2753637103368,
12.0886563476342));
#147915=CARTESIAN_POINT('Ctrl Pts',(17.5808520242221,-21.2375742704973,
12.0928409820273));
#147916=CARTESIAN_POINT('Ctrl Pts',(17.5060588186775,-21.1998386192481,
12.0970196601112));
#147917=CARTESIAN_POINT('Ctrl Pts',(17.4330087179883,-21.1583717310105,
12.1011983381951));
#147918=CARTESIAN_POINT('Ctrl Pts',(17.3620964471735,-21.113360830991,12.1053770162791));
#147919=CARTESIAN_POINT('Ctrl Pts',(17.289913124868,-21.0675431429373,12.1096305941645));
#147920=CARTESIAN_POINT('Ctrl Pts',(17.2199454771429,-21.018053314544,12.11388417205));
#147921=CARTESIAN_POINT('Ctrl Pts',(17.1525850704414,-20.9651385497698,
12.1181377499354));
#147922=CARTESIAN_POINT('Ctrl Pts',(17.0865305766668,-20.9132496409654,
12.1223088639133));
#147923=CARTESIAN_POINT('Ctrl Pts',(17.0229835115634,-20.8580677061308,
12.1264799778913));
#147924=CARTESIAN_POINT('Ctrl Pts',(16.9622836350606,-20.7998693466276,
12.1306510918693));
#147925=CARTESIAN_POINT('Ctrl Pts',(16.9016041269875,-20.741690516146,12.1348208061896));
#147926=CARTESIAN_POINT('Ctrl Pts',(16.8437702418585,-20.6804975893352,
12.13899052051));
#147927=CARTESIAN_POINT('Ctrl Pts',(16.7890867147049,-20.6166057529284,
12.1431602348304));
#147928=CARTESIAN_POINT('Ctrl Pts',(16.7344051334259,-20.5527161900675,
12.1473298007744));
#147929=CARTESIAN_POINT('Ctrl Pts',(16.682873985715,-20.4861282586161,12.1514993667185));
#147930=CARTESIAN_POINT('Ctrl Pts',(16.6347584444192,-20.4171910767278,
12.1556689326625));
#147931=CARTESIAN_POINT('Ctrl Pts',(16.5849512200484,-20.3458301485675,
12.1599850954014));
#147932=CARTESIAN_POINT('Ctrl Pts',(16.5388045582795,-20.2719521294865,
12.1643012581404));
#147933=CARTESIAN_POINT('Ctrl Pts',(16.496563301095,-20.1959762933404,12.1686174208793));
#147934=CARTESIAN_POINT('Ctrl Pts',(16.4556980484202,-20.1224753620654,
12.172792985071));
#147935=CARTESIAN_POINT('Ctrl Pts',(16.4184878365308,-20.0470116310055,
12.1769685492626));
#147936=CARTESIAN_POINT('Ctrl Pts',(16.3851063117009,-19.9699874464201,
12.1811441134543));
#147937=CARTESIAN_POINT('Ctrl Pts',(16.350038765409,-19.8890729533789,12.1855305754669));
#147938=CARTESIAN_POINT('Ctrl Pts',(16.3191970489118,-19.8064367740456,
12.1899170374794));
#147939=CARTESIAN_POINT('Ctrl Pts',(16.2927234637601,-19.7225639970856,
12.1943034994919));
#147940=CARTESIAN_POINT('Ctrl Pts',(16.2662498786084,-19.6386912201256,
12.1986899615045));
#147941=CARTESIAN_POINT('Ctrl Pts',(16.2441444970407,-19.5535824262448,
12.203076423517));
#147942=CARTESIAN_POINT('Ctrl Pts',(16.2264874578015,-19.4677333135615,
12.2074628855296));
#147943=CARTESIAN_POINT('Ctrl Pts',(16.2025156137684,-19.3511814097151,
12.2134181072288));
#147944=CARTESIAN_POINT('Ctrl Pts',(16.1866633864905,-19.2329068373031,
12.219373328928));
#147945=CARTESIAN_POINT('Ctrl Pts',(16.1791211349008,-19.1138455580776,
12.2253285506272));
#147946=CARTESIAN_POINT('Ctrl Pts',(16.1757600463668,-19.060787728371,12.2279824036753));
#147947=CARTESIAN_POINT('Ctrl Pts',(16.1740486686438,-19.0075739736056,
12.2306362567234));
#147948=CARTESIAN_POINT('Ctrl Pts',(16.174001023388,-18.9542890490546,12.2332901097715));
#147949=CARTESIAN_POINT('',(16.1740007840082,-18.949996472737,12.1667098902285));
#147950=CARTESIAN_POINT('Ctrl Pts',(20.2935357468249,-20.9821350335323,
11.8833305117342));
#147951=CARTESIAN_POINT('Ctrl Pts',(20.2268566585352,-21.0333574497933,
11.8875000047157));
#147952=CARTESIAN_POINT('Ctrl Pts',(20.1576368543504,-21.0813024786675,
11.8916694976972));
#147953=CARTESIAN_POINT('Ctrl Pts',(20.0862362138371,-21.1257196741962,
11.8958389906787));
#147954=CARTESIAN_POINT('Ctrl Pts',(20.0148284980351,-21.1701412711487,
11.9000088968269));
#147955=CARTESIAN_POINT('Ctrl Pts',(19.9412399081108,-21.2110340987355,
11.9041788029752));
#147956=CARTESIAN_POINT('Ctrl Pts',(19.8658573753418,-21.2481922571693,
11.9083487091234));
#147957=CARTESIAN_POINT('Ctrl Pts',(19.7903949052723,-21.285389818934,11.912523037132));
#147958=CARTESIAN_POINT('Ctrl Pts',(19.7131351076393,-21.3188446006788,
11.9166973651407));
#147959=CARTESIAN_POINT('Ctrl Pts',(19.6344870159503,-21.3483979498625,
11.9208716931493));
#147960=CARTESIAN_POINT('Ctrl Pts',(19.5557947538892,-21.3779678968097,
11.9250483655457));
#147961=CARTESIAN_POINT('Ctrl Pts',(19.4757130835543,-21.4036319081676,
11.9292250379421));
#147962=CARTESIAN_POINT('Ctrl Pts',(19.3946660856504,-21.4252812867265,
11.9334017103385));
#147963=CARTESIAN_POINT('Ctrl Pts',(19.3134800547385,-21.4469678039617,
11.9375855476558));
#147964=CARTESIAN_POINT('Ctrl Pts',(19.2313258391223,-21.4646258381512,
11.9417693849731));
#147965=CARTESIAN_POINT('Ctrl Pts',(19.1486373175954,-21.478197912844,11.9459532222903));
#147966=CARTESIAN_POINT('Ctrl Pts',(19.0921615639953,-21.4874675567079,
11.9488107575452));
#147967=CARTESIAN_POINT('Ctrl Pts',(19.0354367233637,-21.4948322630722,
11.9516682928));
#147968=CARTESIAN_POINT('Ctrl Pts',(18.9786013944249,-21.5002876913421,
11.9545258280548));
#147969=CARTESIAN_POINT('Ctrl Pts',(18.8953705500055,-21.5082767346017,
11.9587104624479));
#147970=CARTESIAN_POINT('Ctrl Pts',(18.8115930039276,-21.5121986934545,
11.9628950968409));
#147971=CARTESIAN_POINT('Ctrl Pts',(18.7277003248363,-21.5119922488345,
11.967079731234));
#147972=CARTESIAN_POINT('Ctrl Pts',(18.6439270565898,-21.5117860980629,
11.9712584093179));
#147973=CARTESIAN_POINT('Ctrl Pts',(18.560039436939,-21.507463217065,11.9754370874018));
#147974=CARTESIAN_POINT('Ctrl Pts',(18.4764742375282,-21.4990140324826,
11.9796157654858));
#147975=CARTESIAN_POINT('Ctrl Pts',(18.391411191975,-21.4904134023389,11.9838693433712));
#147976=CARTESIAN_POINT('Ctrl Pts',(18.3066827190521,-21.4775370395473,
11.9881229212567));
#147977=CARTESIAN_POINT('Ctrl Pts',(18.2227496524054,-21.460430402081,11.9923764991421));
#147978=CARTESIAN_POINT('Ctrl Pts',(18.1404437920376,-21.4436554101629,
11.99654761312));
#147979=CARTESIAN_POINT('Ctrl Pts',(18.0589032436853,-21.4228128002076,
12.000718727098));
#147980=CARTESIAN_POINT('Ctrl Pts',(17.9785557081133,-21.3979975310404,
12.004889841076));
#147981=CARTESIAN_POINT('Ctrl Pts',(17.898235133933,-21.3731905888765,12.0090595553963));
#147982=CARTESIAN_POINT('Ctrl Pts',(17.819107216658,-21.3444137706279,12.0132292697167));
#147983=CARTESIAN_POINT('Ctrl Pts',(17.7415856439041,-21.3118122268127,
12.0173989840371));
#147984=CARTESIAN_POINT('Ctrl Pts',(17.6640668297004,-21.2792118431003,
12.0215685499811));
#147985=CARTESIAN_POINT('Ctrl Pts',(17.5881546700965,-21.2427871835461,
12.0257381159252));
#147986=CARTESIAN_POINT('Ctrl Pts',(17.5142426975068,-21.2027314639944,
12.0299076818692));
#147987=CARTESIAN_POINT('Ctrl Pts',(17.4377320711412,-21.1612674347574,
12.0342238446081));
#147988=CARTESIAN_POINT('Ctrl Pts',(17.3633653656329,-21.1159125099135,
12.0385400073471));
#147989=CARTESIAN_POINT('Ctrl Pts',(17.2915493867665,-21.0669317313763,
12.042856170086));
#147990=CARTESIAN_POINT('Ctrl Pts',(17.222072805858,-21.0195464965481,12.0470317342777));
#147991=CARTESIAN_POINT('Ctrl Pts',(17.1549836708369,-20.968768326667,12.0512072984694));
#147992=CARTESIAN_POINT('Ctrl Pts',(17.0906175572636,-20.914879045409,12.055382862661));
#147993=CARTESIAN_POINT('Ctrl Pts',(17.0230004643097,-20.8582679446643,
12.0597693246736));
#147994=CARTESIAN_POINT('Ctrl Pts',(16.9583891293619,-20.7982235859986,
12.0641557866861));
#147995=CARTESIAN_POINT('Ctrl Pts',(16.8971281979621,-20.735115807478,12.0685422486987));
#147996=CARTESIAN_POINT('Ctrl Pts',(16.8358672665623,-20.6720080289574,
12.0729287107112));
#147997=CARTESIAN_POINT('Ctrl Pts',(16.7779570635865,-20.6058373172987,
12.0773151727238));
#147998=CARTESIAN_POINT('Ctrl Pts',(16.7236914224212,-20.5370108589259,
12.0817016347363));
#147999=CARTESIAN_POINT('Ctrl Pts',(16.6719732357611,-20.4714154002739,
12.0858821780095));
#148000=CARTESIAN_POINT('Ctrl Pts',(16.62336875941,-20.403158891998,12.0900627212828));
#148001=CARTESIAN_POINT('Ctrl Pts',(16.5781640651477,-20.3325692383938,
12.094243264556));
#148002=CARTESIAN_POINT('Ctrl Pts',(16.5330221281564,-20.2620775837719,
12.0984180040186));
#148003=CARTESIAN_POINT('Ctrl Pts',(16.4912708487477,-20.1892595981085,
12.1025927434812));
#148004=CARTESIAN_POINT('Ctrl Pts',(16.4531558825332,-20.1144758542942,
12.1067674829437));
#148005=CARTESIAN_POINT('Ctrl Pts',(16.4150823671081,-20.0397734392997,
12.1109376822935));
#148006=CARTESIAN_POINT('Ctrl Pts',(16.380637519025,-19.9631099194743,12.1151078816432));
#148007=CARTESIAN_POINT('Ctrl Pts',(16.3500227648594,-19.8848732723855,
12.119278080993));
#148008=CARTESIAN_POINT('Ctrl Pts',(16.319430601241,-19.8066943559144,12.1234452031635));
#148009=CARTESIAN_POINT('Ctrl Pts',(16.2926630858425,-19.7269450449961,
12.1276123253341));
#148010=CARTESIAN_POINT('Ctrl Pts',(16.2698743296479,-19.6460350716728,
12.1317794475046));
#148011=CARTESIAN_POINT('Ctrl Pts',(16.2470959536797,-19.5651619526576,
12.1359446715605));
#148012=CARTESIAN_POINT('Ctrl Pts',(16.2282928589745,-19.4831296648129,
12.1401098956164));
#148013=CARTESIAN_POINT('Ctrl Pts',(16.2135694674,-19.4003636139762,12.1442751196724));
#148014=CARTESIAN_POINT('Ctrl Pts',(16.1988435352848,-19.3175832817472,
12.1484410624432));
#148015=CARTESIAN_POINT('Ctrl Pts',(16.1881988016354,-19.2340693856754,
12.1526070052141));
#148016=CARTESIAN_POINT('Ctrl Pts',(16.1816884763611,-19.1502571216887,
12.156772947985));
#148017=CARTESIAN_POINT('Ctrl Pts',(16.1765121589547,-19.0836185341113,
12.1600852620661));
#148018=CARTESIAN_POINT('Ctrl Pts',(16.1739485082683,-19.0167915973248,
12.1633975761473));
#148019=CARTESIAN_POINT('Ctrl Pts',(16.1740007840082,-18.949996472737,12.1667098902285));
#148020=CARTESIAN_POINT('Ctrl Pts',(16.1763510013672,-18.9499800105097,
12.1667107986216));
#148021=CARTESIAN_POINT('Ctrl Pts',(16.1742902547169,-18.6667985525942,
12.1807663462203));
#148022=CARTESIAN_POINT('Ctrl Pts',(16.3483939296849,-17.5319993745477,
12.2372138293795));
#148023=CARTESIAN_POINT('Ctrl Pts',(18.012168501089,-16.0122294088113,12.3360532480991));
#148024=CARTESIAN_POINT('Ctrl Pts',(20.815168138664,-16.7538118778759,12.4632290547806));
#148025=CARTESIAN_POINT('Ctrl Pts',(21.6282770393392,-19.2634826679177,
12.5789421029395));
#148026=CARTESIAN_POINT('Ctrl Pts',(20.782749793487,-20.5975255724166,12.652263215538));
#148027=CARTESIAN_POINT('Ctrl Pts',(20.2929505273095,-20.9813917755491,
12.683192392576));
#148028=CARTESIAN_POINT('Origin',(18.734,-18.952,-1.76670989022851));
#148029=CARTESIAN_POINT('',(20.2935357468249,-20.9821350335323,13.5498657043958));
#148030=CARTESIAN_POINT('',(20.2935357468249,-20.9821350335323,13.4833228568185));
#148031=CARTESIAN_POINT('',(20.2935357468249,-20.9821350335323,-1.76670989022851));
#148032=CARTESIAN_POINT('',(16.174000001606,-18.9520906788002,13.0332901097364));
#148033=CARTESIAN_POINT('Ctrl Pts',(16.174000001606,-18.9520906780897,13.0332901097715));
#148034=CARTESIAN_POINT('Ctrl Pts',(16.1739968821085,-18.8640218456489,
13.0376462156856));
#148035=CARTESIAN_POINT('Ctrl Pts',(16.1785426714359,-18.776035607655,13.0420023215996));
#148036=CARTESIAN_POINT('Ctrl Pts',(16.1875860737584,-18.6886065372053,
13.0463584275137));
#148037=CARTESIAN_POINT('Ctrl Pts',(16.1966529338892,-18.6009506832622,
13.050725832792));
#148038=CARTESIAN_POINT('Ctrl Pts',(16.2102406836425,-18.5138552818865,
13.0550932380704));
#148039=CARTESIAN_POINT('Ctrl Pts',(16.2282463851318,-18.4277874271108,
13.0594606433487));
#148040=CARTESIAN_POINT('Ctrl Pts',(16.2462755658188,-18.3416073409855,
13.0638337436661));
#148041=CARTESIAN_POINT('Ctrl Pts',(16.2687340840993,-18.2564578570398,
13.0682068439834));
#148042=CARTESIAN_POINT('Ctrl Pts',(16.2954690366781,-18.1727909517206,
13.0725799443007));
#148043=CARTESIAN_POINT('Ctrl Pts',(16.3222767415772,-18.0888963683653,
13.0769649448896));
#148044=CARTESIAN_POINT('Ctrl Pts',(16.3533840099471,-18.0064928038111,
13.0813499454785));
#148045=CARTESIAN_POINT('Ctrl Pts',(16.3885892814888,-17.9260133716794,
13.0857349460673));
#148046=CARTESIAN_POINT('Ctrl Pts',(16.4205927188907,-17.8528533488879,
13.0897211414781));
#148047=CARTESIAN_POINT('Ctrl Pts',(16.4559819492917,-17.7812832866316,
13.0937073368888));
#148048=CARTESIAN_POINT('Ctrl Pts',(16.4945737975983,-17.7116088181558,
13.0976935322996));
#148049=CARTESIAN_POINT('Ctrl Pts',(16.5350868078939,-17.638465846711,13.1018781666926));
#148050=CARTESIAN_POINT('Ctrl Pts',(16.5792624158945,-17.5671736686978,
13.1060628010856));
#148051=CARTESIAN_POINT('Ctrl Pts',(16.6269069559,-17.4981228031552,13.1102474354787));
#148052=CARTESIAN_POINT('Ctrl Pts',(16.6744836797999,-17.4291702229729,
13.1144261135626));
#148053=CARTESIAN_POINT('Ctrl Pts',(16.7255192690589,-17.3624529938655,
13.1186047916466));
#148054=CARTESIAN_POINT('Ctrl Pts',(16.779774450421,-17.2983366420662,13.1227834697305));
#148055=CARTESIAN_POINT('Ctrl Pts',(16.8350021169166,-17.2330710507404,
13.1270370476159));
#148056=CARTESIAN_POINT('Ctrl Pts',(16.8935656995715,-17.1705009170566,
13.1312906255014));
#148057=CARTESIAN_POINT('Ctrl Pts',(16.9551669364595,-17.110980463967,13.1355442033868));
#148058=CARTESIAN_POINT('Ctrl Pts',(17.0155739131654,-17.0526139310053,
13.1397153173648));
#148059=CARTESIAN_POINT('Ctrl Pts',(17.0789014673906,-16.9971802202222,
13.1438864313427));
#148060=CARTESIAN_POINT('Ctrl Pts',(17.1448292745175,-16.9449782250136,
13.1480575453207));
#148061=CARTESIAN_POINT('Ctrl Pts',(17.210734958932,-16.8927937466887,13.152227259641));
#148062=CARTESIAN_POINT('Ctrl Pts',(17.2792388030076,-16.8438391155733,
13.1563969739614));
#148063=CARTESIAN_POINT('Ctrl Pts',(17.3499870301182,-16.7983732683682,
13.1605666882818));
#148064=CARTESIAN_POINT('Ctrl Pts',(17.4207327397034,-16.752909039033,13.1647362542258));
#148065=CARTESIAN_POINT('Ctrl Pts',(17.4937222860637,-16.7109335947648,
13.1689058201699));
#148066=CARTESIAN_POINT('Ctrl Pts',(17.5685736694551,-16.6726620548781,
13.1730753861139));
#148067=CARTESIAN_POINT('Ctrl Pts',(17.6460567351474,-16.633044934862,13.1773915488529));
#148068=CARTESIAN_POINT('Ctrl Pts',(17.7255345286223,-16.5973972639688,
13.1817077115918));
#148069=CARTESIAN_POINT('Ctrl Pts',(17.8065583197872,-16.5659044592045,
13.1860238743307));
#148070=CARTESIAN_POINT('Ctrl Pts',(17.884942769477,-16.535437529243,13.1901994385224));
#148071=CARTESIAN_POINT('Ctrl Pts',(17.9647735800335,-16.508859036806,13.1943750027141));
#148072=CARTESIAN_POINT('Ctrl Pts',(18.0456284938941,-16.4862861744352,
13.1985505669057));
#148073=CARTESIAN_POINT('Ctrl Pts',(18.1305671972396,-16.4625732104479,
13.2029370289183));
#148074=CARTESIAN_POINT('Ctrl Pts',(18.2166356079045,-16.4432812873466,
13.2073234909308));
#148075=CARTESIAN_POINT('Ctrl Pts',(18.3033337697291,-16.4284852688949,
13.2117099529434));
#148076=CARTESIAN_POINT('Ctrl Pts',(18.3900319315537,-16.4136892504433,
13.2160964149559));
#148077=CARTESIAN_POINT('Ctrl Pts',(18.4773592594053,-16.4033891290646,
13.2204828769685));
#148078=CARTESIAN_POINT('Ctrl Pts',(18.5648137584887,-16.3975967398073,
13.224869338981));
#148079=CARTESIAN_POINT('Ctrl Pts',(18.6482443464305,-16.3920708669661,
13.2290539733741));
#148080=CARTESIAN_POINT('Ctrl Pts',(18.7321012046619,-16.3906264585577,
13.2332386077671));
#148081=CARTESIAN_POINT('Ctrl Pts',(18.8159511409017,-16.3933120529254,
13.2374232421602));
#148082=CARTESIAN_POINT('Ctrl Pts',(18.8996817271358,-16.3959938246819,
13.2416019202441));
#148083=CARTESIAN_POINT('Ctrl Pts',(18.9834049550842,-16.4027939079682,
13.245780598328));
#148084=CARTESIAN_POINT('Ctrl Pts',(19.0666839609553,-16.413708964259,13.249959276412));
#148085=CARTESIAN_POINT('Ctrl Pts',(19.151455683155,-16.4248196650893,13.2542128542974));
#148086=CARTESIAN_POINT('Ctrl Pts',(19.2357666201897,-16.4401943435876,
13.2584664321829));
#148087=CARTESIAN_POINT('Ctrl Pts',(19.3191574830896,-16.4597739428406,
13.2627200100683));
#148088=CARTESIAN_POINT('Ctrl Pts',(19.4009316513885,-16.4789739533557,
13.2668911240463));
#148089=CARTESIAN_POINT('Ctrl Pts',(19.4818206335823,-16.502217188393,13.2710622380242));
#148090=CARTESIAN_POINT('Ctrl Pts',(19.561399721986,-16.5293960909679,13.2752333520022));
#148091=CARTESIAN_POINT('Ctrl Pts',(19.6409521068579,-16.5565658733995,
13.2794030663226));
#148092=CARTESIAN_POINT('Ctrl Pts',(19.7191950359075,-16.5876685519741,
13.2835727806429));
#148093=CARTESIAN_POINT('Ctrl Pts',(19.7957192917694,-16.6225468140603,
13.2877424949633));
#148094=CARTESIAN_POINT('Ctrl Pts',(19.8722408245699,-16.6574238350283,
13.2919120609074));
#148095=CARTESIAN_POINT('Ctrl Pts',(19.9470433875299,-16.6960759808161,
13.2960816268514));
#148096=CARTESIAN_POINT('Ctrl Pts',(20.019739330133,-16.7382984900965,13.3002511927954));
#148097=CARTESIAN_POINT('Ctrl Pts',(20.0949911723979,-16.7820054907161,
13.3045673555344));
#148098=CARTESIAN_POINT('Ctrl Pts',(20.1679850444452,-16.8295383292521,
13.3088835182733));
#148099=CARTESIAN_POINT('Ctrl Pts',(20.2383221508273,-16.8806200574181,
13.3131996810122));
#148100=CARTESIAN_POINT('Ctrl Pts',(20.3063680333671,-16.9300378036621,
13.3173752452039));
#148101=CARTESIAN_POINT('Ctrl Pts',(20.3719272430123,-16.9827764479853,
13.3215508093956));
#148102=CARTESIAN_POINT('Ctrl Pts',(20.4346726793713,-17.0385443727015,
13.3257263735873));
#148103=CARTESIAN_POINT('Ctrl Pts',(20.5005872385575,-17.0971290027194,
13.3301128355998));
#148104=CARTESIAN_POINT('Ctrl Pts',(20.5633958911489,-17.1590565633927,
13.3344992976123));
#148105=CARTESIAN_POINT('Ctrl Pts',(20.6227650717809,-17.2239471930463,
13.3388857596249));
#148106=CARTESIAN_POINT('Ctrl Pts',(20.6821342524129,-17.2888378226999,
13.3432722216374));
#148107=CARTESIAN_POINT('Ctrl Pts',(20.738063650735,-17.3566910252287,13.3476586836499));
#148108=CARTESIAN_POINT('Ctrl Pts',(20.7902715950829,-17.4270911085396,
13.3520451456625));
#148109=CARTESIAN_POINT('Ctrl Pts',(20.8400773745207,-17.4942519796594,
13.3562297800555));
#148110=CARTESIAN_POINT('Ctrl Pts',(20.8866820202992,-17.5639804959204,
13.3604144144486));
#148111=CARTESIAN_POINT('Ctrl Pts',(20.9298102405872,-17.6359386840529,
13.3645990488416));
#148112=CARTESIAN_POINT('Ctrl Pts',(20.9728770731919,-17.7077944486113,
13.3687777269256));
#148113=CARTESIAN_POINT('Ctrl Pts',(21.0124770746365,-17.7818731899369,
13.3729564050095));
#148114=CARTESIAN_POINT('Ctrl Pts',(21.0483765860078,-17.8578057676359,
13.3771350830935));
#148115=CARTESIAN_POINT('Ctrl Pts',(21.0849195703199,-17.9350993822183,
13.3813886609789));
#148116=CARTESIAN_POINT('Ctrl Pts',(21.1176278099319,-18.0143135596366,
13.3856422388643));
#148117=CARTESIAN_POINT('Ctrl Pts',(21.1463023579538,-18.0950301441645,
13.3898958167498));
#148118=CARTESIAN_POINT('Ctrl Pts',(21.1744209939084,-18.1741818801958,
13.3940669307277));
#148119=CARTESIAN_POINT('Ctrl Pts',(21.1986607834443,-18.2547778355445,
13.3982380447057));
#148120=CARTESIAN_POINT('Ctrl Pts',(21.2188822787495,-18.3364026797032,
13.4024091586836));
#148121=CARTESIAN_POINT('Ctrl Pts',(21.2390969885367,-18.4180001338572,
13.406578873004));
#148122=CARTESIAN_POINT('Ctrl Pts',(21.2552959714612,-18.5006253449795,
13.4107485873244));
#148123=CARTESIAN_POINT('Ctrl Pts',(21.2673900009521,-18.5838490756821,
13.4149183016447));
#148124=CARTESIAN_POINT('Ctrl Pts',(21.2794836000854,-18.6670698449271,
13.4190878675888));
#148125=CARTESIAN_POINT('Ctrl Pts',(21.2874724709,-18.7508886360331,13.4232574335328));
#148126=CARTESIAN_POINT('Ctrl Pts',(21.2913189573956,-18.8348686628402,
13.4274269994769));
#148127=CARTESIAN_POINT('Ctrl Pts',(21.2953006816113,-18.9218013237893,
13.4317431622158));
#148128=CARTESIAN_POINT('Ctrl Pts',(21.2948432851383,-19.0089062426184,
13.4360593249547));
#148129=CARTESIAN_POINT('Ctrl Pts',(21.2899637772452,-19.095698188612,13.4403754876936));
#148130=CARTESIAN_POINT('Ctrl Pts',(21.2852432188086,-19.1796628960938,
13.4445510518853));
#148131=CARTESIAN_POINT('Ctrl Pts',(21.2763843217563,-19.2633342443401,
13.448726616077));
#148132=CARTESIAN_POINT('Ctrl Pts',(21.2634552371752,-19.3462793465638,
13.4529021802687));
#148133=CARTESIAN_POINT('Ctrl Pts',(21.249873135268,-19.4334138087177,13.4572886422812));
#148134=CARTESIAN_POINT('Ctrl Pts',(21.2317989893781,-19.5197461599058,
13.4616751042937));
#148135=CARTESIAN_POINT('Ctrl Pts',(21.2093716504546,-19.6047903125242,
13.4660615663063));
#148136=CARTESIAN_POINT('Ctrl Pts',(21.1869443115312,-19.6898344651427,
13.4704480283188));
#148137=CARTESIAN_POINT('Ctrl Pts',(21.1601640287334,-19.7735898897036,
13.4748344903314));
#148138=CARTESIAN_POINT('Ctrl Pts',(21.1292278697972,-19.855594738667,13.4792209523439));
#148139=CARTESIAN_POINT('Ctrl Pts',(21.0997172163826,-19.9338208908233,
13.483405290821));
#148140=CARTESIAN_POINT('Ctrl Pts',(21.0663154177823,-20.0107453980514,
13.487589629298));
#148141=CARTESIAN_POINT('Ctrl Pts',(21.0291576153325,-20.0859539323894,
13.491773967775));
#148142=CARTESIAN_POINT('Ctrl Pts',(20.9920502936115,-20.1610602921805,
13.4959526216194));
#148143=CARTESIAN_POINT('Ctrl Pts',(20.9511973024599,-20.2344548993957,
13.5001312754638));
#148144=CARTESIAN_POINT('Ctrl Pts',(20.9067825486354,-20.3057414806179,
13.5043099293083));
#148145=CARTESIAN_POINT('Ctrl Pts',(20.862419706075,-20.3769447432077,13.5084836992079));
#148146=CARTESIAN_POINT('Ctrl Pts',(20.8145036176995,-20.4460444889432,
13.5126574691076));
#148147=CARTESIAN_POINT('Ctrl Pts',(20.7632642938657,-20.512668582897,13.5168312390073));
#148148=CARTESIAN_POINT('Ctrl Pts',(20.7120601643895,-20.5792469152753,
13.5210021421019));
#148149=CARTESIAN_POINT('Ctrl Pts',(20.657537612992,-20.6433526098853,13.5251730451966));
#148150=CARTESIAN_POINT('Ctrl Pts',(20.5999695483209,-20.7046430454428,
13.5293439482913));
#148151=CARTESIAN_POINT('Ctrl Pts',(20.5424157972175,-20.7659182419125,
13.5335138143439));
#148152=CARTESIAN_POINT('Ctrl Pts',(20.4818183469846,-20.8243792304162,
13.5376836803965));
#148153=CARTESIAN_POINT('Ctrl Pts',(20.4184891456872,-20.8797179041712,
13.5418535464491));
#148154=CARTESIAN_POINT('Ctrl Pts',(20.3779280055904,-20.9151612644688,
13.5445242657647));
#148155=CARTESIAN_POINT('Ctrl Pts',(20.3362470404378,-20.9493245120241,
13.5471949850803));
#148156=CARTESIAN_POINT('Ctrl Pts',(20.2935357468249,-20.9821350335323,
13.5498657043958));
#148157=CARTESIAN_POINT('Ctrl Pts',(20.2935357468249,-20.9821350335323,
12.7499597608822));
#148158=CARTESIAN_POINT('Ctrl Pts',(20.226946636523,-21.0332883293229,12.7541315972059));
#148159=CARTESIAN_POINT('Ctrl Pts',(20.1577807455201,-21.0812060335431,
12.7583034335296));
#148160=CARTESIAN_POINT('Ctrl Pts',(20.0863882307441,-21.1256250995387,
12.7624752698533));
#148161=CARTESIAN_POINT('Ctrl Pts',(20.0150266132867,-21.17002494181,12.7666453006858));
#148162=CARTESIAN_POINT('Ctrl Pts',(19.9414406756441,-21.2109289098134,
12.7708153315183));
#148163=CARTESIAN_POINT('Ctrl Pts',(19.8660096662966,-21.2481171824215,
12.7749853623508));
#148164=CARTESIAN_POINT('Ctrl Pts',(19.7905886744805,-21.2853005162823,
12.779154839387));
#148165=CARTESIAN_POINT('Ctrl Pts',(19.713323510543,-21.3187689321608,12.7833243164232));
#148166=CARTESIAN_POINT('Ctrl Pts',(19.6346169149111,-21.3483491341155,
12.7874937934594));
#148167=CARTESIAN_POINT('Ctrl Pts',(19.5558971620611,-21.3779342809311,
12.7916639674985));
#148168=CARTESIAN_POINT('Ctrl Pts',(19.4757359300974,-21.4036297625856,
12.7958341415375));
#148169=CARTESIAN_POINT('Ctrl Pts',(19.3945534755297,-21.4253113645406,
12.8000043155765));
#148170=CARTESIAN_POINT('Ctrl Pts',(19.3132817233196,-21.4470168154411,
12.8041790766499));
#148171=CARTESIAN_POINT('Ctrl Pts',(19.2309869517452,-21.4646994560134,
12.8083538377233));
#148172=CARTESIAN_POINT('Ctrl Pts',(19.1481015024818,-21.4782858004672,
12.8125285987966));
#148173=CARTESIAN_POINT('Ctrl Pts',(19.0651644433043,-21.4918806046697,
12.81670595935));
#148174=CARTESIAN_POINT('Ctrl Pts',(18.9816364311649,-21.5013739840884,
12.8208833199033));
#148175=CARTESIAN_POINT('Ctrl Pts',(18.8979544650464,-21.5067443968803,
12.8250606804566));
#148176=CARTESIAN_POINT('Ctrl Pts',(18.8141346684161,-21.5121236551472,
12.8292449214379));
#148177=CARTESIAN_POINT('Ctrl Pts',(18.7301608710164,-21.5133663855053,
12.8334291624192));
#148178=CARTESIAN_POINT('Ctrl Pts',(18.6464691654977,-21.5105031469614,
12.8376134034005));
#148179=CARTESIAN_POINT('Ctrl Pts',(18.608275919502,-21.5091964897082,12.8395229085792));
#148180=CARTESIAN_POINT('Ctrl Pts',(18.5701413376032,-21.5070354322662,
12.8414324137579));
#148181=CARTESIAN_POINT('Ctrl Pts',(18.5321062576875,-21.5040264334084,
12.8433419189367));
#148182=CARTESIAN_POINT('Ctrl Pts',(18.4487533004234,-21.497432285223,12.8475265533297));
#148183=CARTESIAN_POINT('Ctrl Pts',(18.3655686284663,-21.4867379250515,
12.8517111877228));
#148184=CARTESIAN_POINT('Ctrl Pts',(18.2829879003454,-21.4719579532137,
12.8558958221158));
#148185=CARTESIAN_POINT('Ctrl Pts',(18.2005247156697,-21.4571990188365,
12.8600745001997));
#148186=CARTESIAN_POINT('Ctrl Pts',(18.1186642162802,-21.4383661042868,
12.8642531782836));
#148187=CARTESIAN_POINT('Ctrl Pts',(18.0378381935519,-21.4155256725358,
12.8684318563676));
#148188=CARTESIAN_POINT('Ctrl Pts',(17.9555634224545,-21.3922758424606,
12.872685434253));
#148189=CARTESIAN_POINT('Ctrl Pts',(17.8743610594202,-21.3648734505898,
12.8769390121385));
#148190=CARTESIAN_POINT('Ctrl Pts',(17.7946770299223,-21.3334433350144,
12.8811925900239));
#148191=CARTESIAN_POINT('Ctrl Pts',(17.7165378308269,-21.3026225535603,
12.8853637040018));
#148192=CARTESIAN_POINT('Ctrl Pts',(17.6398590665665,-21.2679290019,12.8895348179798));
#148193=CARTESIAN_POINT('Ctrl Pts',(17.5650454327543,-21.2295305090636,
12.8937059319577));
#148194=CARTESIAN_POINT('Ctrl Pts',(17.4902569033794,-21.1911449012122,
12.8978756462781));
#148195=CARTESIAN_POINT('Ctrl Pts',(17.4173326704122,-21.1490570311436,
12.9020453605985));
#148196=CARTESIAN_POINT('Ctrl Pts',(17.3466549084741,-21.103481721284,12.9062150749189));
#148197=CARTESIAN_POINT('Ctrl Pts',(17.2759796615542,-21.0579080331895,
12.9103846408629));
#148198=CARTESIAN_POINT('Ctrl Pts',(17.2075511128842,-21.0088474020655,
12.9145542068069));
#148199=CARTESIAN_POINT('Ctrl Pts',(17.1417232369321,-20.9565584825078,
12.918723772751));
#148200=CARTESIAN_POINT('Ctrl Pts',(17.0735809340688,-20.9024311490436,
12.9230399354899));
#148201=CARTESIAN_POINT('Ctrl Pts',(17.008225998861,-20.8448446181552,12.9273560982288));
#148202=CARTESIAN_POINT('Ctrl Pts',(16.9460129971983,-20.7841305842686,
12.9316722609678));
#148203=CARTESIAN_POINT('Ctrl Pts',(16.8858265775214,-20.72539430365,12.9358478251594));
#148204=CARTESIAN_POINT('Ctrl Pts',(16.8285808237904,-20.6637315251358,
12.9400233893511));
#148205=CARTESIAN_POINT('Ctrl Pts',(16.7745572392503,-20.5994780931307,
12.9441989535428));
#148206=CARTESIAN_POINT('Ctrl Pts',(16.7178050518837,-20.5319793730228,
12.9485854155553));
#148207=CARTESIAN_POINT('Ctrl Pts',(16.6646094437673,-20.4616218795449,
12.9529718775679));
#148208=CARTESIAN_POINT('Ctrl Pts',(16.6152455573352,-20.38882970866,12.9573583395805));
#148209=CARTESIAN_POINT('Ctrl Pts',(16.5658816709031,-20.3160375377752,
12.961744801593));
#148210=CARTESIAN_POINT('Ctrl Pts',(16.5203497415207,-20.2408112252451,
12.9661312636056));
#148211=CARTESIAN_POINT('Ctrl Pts',(16.4788683829465,-20.1636028184871,
12.9705177256181));
#148212=CARTESIAN_POINT('Ctrl Pts',(16.4371381237558,-20.0859311380873,
12.9749305077209));
#148213=CARTESIAN_POINT('Ctrl Pts',(16.3993648293879,-20.0059905501582,
12.9793432898236));
#148214=CARTESIAN_POINT('Ctrl Pts',(16.3657873879881,-19.9241980375972,
12.9837560719264));
#148215=CARTESIAN_POINT('Ctrl Pts',(16.3323070847553,-19.8426421474352,
12.9881560880307));
#148216=CARTESIAN_POINT('Ctrl Pts',(16.302998596953,-19.7592453620159,12.9925561041351));
#148217=CARTESIAN_POINT('Ctrl Pts',(16.278054237255,-19.6744475139794,12.9969561202394));
#148218=CARTESIAN_POINT('Ctrl Pts',(16.2531532512186,-19.5897971138313,
13.0013484855236));
#148219=CARTESIAN_POINT('Ctrl Pts',(16.2326014031163,-19.5037508664346,
13.0057408508078));
#148220=CARTESIAN_POINT('Ctrl Pts',(16.2165427462274,-19.4167676574675,
13.010133216092));
#148221=CARTESIAN_POINT('Ctrl Pts',(16.200521001668,-19.3299843875664,13.0145154851125));
#148222=CARTESIAN_POINT('Ctrl Pts',(16.1889719431305,-19.2422688247292,
13.018897754133));
#148223=CARTESIAN_POINT('Ctrl Pts',(16.1819893075699,-19.1540926166946,
13.0232800231536));
#148224=CARTESIAN_POINT('Ctrl Pts',(16.176672671659,-19.0869545296414,13.0266167186812));
#148225=CARTESIAN_POINT('Ctrl Pts',(16.1740023911013,-19.0195497546633,
13.0299534142088));
#148226=CARTESIAN_POINT('Ctrl Pts',(16.174000001606,-18.9520906788001,13.0332901097364));
#148227=CARTESIAN_POINT('',(16.1736697275687,-18.9513574892655,12.9667098340851));
#148228=CARTESIAN_POINT('Ctrl Pts',(20.2929505273095,-20.9813917755491,
12.683192392576));
#148229=CARTESIAN_POINT('Ctrl Pts',(20.11142449751,-21.1236576232965,12.6946551510985));
#148230=CARTESIAN_POINT('Ctrl Pts',(19.1726622067198,-21.6766233453797,
12.7485098451814));
#148231=CARTESIAN_POINT('Ctrl Pts',(17.0319370527368,-21.4324760457865,
12.8430154491732));
#148232=CARTESIAN_POINT('Ctrl Pts',(16.1727139550341,-19.7651271422422,
12.9260582946424));
#148233=CARTESIAN_POINT('Ctrl Pts',(16.1699654914217,-18.9513691601896,
12.9667092045512));
#148234=CARTESIAN_POINT('Ctrl Pts',(16.1740000808904,-18.9513564484225,
12.9667098902285));
#148235=CARTESIAN_POINT('Ctrl Pts',(16.1740088273484,-18.9165636940743,
12.9684506873211));
#148236=CARTESIAN_POINT('Ctrl Pts',(16.1747268399112,-18.881780730387,12.9701914844137));
#148237=CARTESIAN_POINT('Ctrl Pts',(16.1761531171477,-18.8470270326105,
12.9719322815063));
#148238=CARTESIAN_POINT('Ctrl Pts',(16.1795816894971,-18.7634839708603,
12.9761169158993));
#148239=CARTESIAN_POINT('Ctrl Pts',(16.1871139062631,-18.6799535889704,
12.9803015502924));
#148240=CARTESIAN_POINT('Ctrl Pts',(16.1987516982625,-18.5968717857769,
12.9844861846854));
#148241=CARTESIAN_POINT('Ctrl Pts',(16.2103729253055,-18.5139082392468,
12.9886648627694));
#148242=CARTESIAN_POINT('Ctrl Pts',(16.2260880567288,-18.4313924548469,
12.9928435408533));
#148243=CARTESIAN_POINT('Ctrl Pts',(16.2458470513543,-18.3497584337278,
12.9970222189372));
#148244=CARTESIAN_POINT('Ctrl Pts',(16.2659602117581,-18.2666611814494,
13.0012757968227));
#148245=CARTESIAN_POINT('Ctrl Pts',(16.2902636140324,-18.1844780963255,
13.0055293747081));
#148246=CARTESIAN_POINT('Ctrl Pts',(16.3186494198465,-18.1036595170853,
13.0097829525935));
#148247=CARTESIAN_POINT('Ctrl Pts',(16.3464849114244,-18.0244077637083,
13.0139540665715));
#148248=CARTESIAN_POINT('Ctrl Pts',(16.3782457689155,-17.9464685351598,
13.0181251805494));
#148249=CARTESIAN_POINT('Ctrl Pts',(16.4137796304914,-17.8702526002262,
13.0222962945274));
#148250=CARTESIAN_POINT('Ctrl Pts',(16.4493015683369,-17.7940622402856,
13.0264660088478));
#148251=CARTESIAN_POINT('Ctrl Pts',(16.4885938016076,-17.7195944421082,
13.0306357231681));
#148252=CARTESIAN_POINT('Ctrl Pts',(16.5314561548595,-17.6472392517271,
13.0348054374885));
#148253=CARTESIAN_POINT('Ctrl Pts',(16.5743169828848,-17.5748866360543,
13.0389750034325));
#148254=CARTESIAN_POINT('Ctrl Pts',(16.6207474431035,-17.5046468740728,
13.0431445693766));
#148255=CARTESIAN_POINT('Ctrl Pts',(16.6705024900493,-17.4368834941077,
13.0473141353206));
#148256=CARTESIAN_POINT('Ctrl Pts',(16.7220068630664,-17.366737637298,13.0516302980595));
#148257=CARTESIAN_POINT('Ctrl Pts',(16.7770736453878,-17.2992459668448,
13.0559464607985));
#148258=CARTESIAN_POINT('Ctrl Pts',(16.8353848266788,-17.234775371818,13.0602626235374));
#148259=CARTESIAN_POINT('Ctrl Pts',(16.8917965273724,-17.1724048996433,
13.0644381877291));
#148260=CARTESIAN_POINT('Ctrl Pts',(16.9512441342268,-17.1128620023875,
13.0686137519207));
#148261=CARTESIAN_POINT('Ctrl Pts',(17.0134027193002,-17.0564407163983,
13.0727893161124));
#148262=CARTESIAN_POINT('Ctrl Pts',(17.078700786738,-16.9971697253824,13.077175778125));
#148263=CARTESIAN_POINT('Ctrl Pts',(17.146990440611,-16.9413443477726,13.0815622401375));
#148264=CARTESIAN_POINT('Ctrl Pts',(17.2178583236867,-16.889255610274,13.0859487021501));
#148265=CARTESIAN_POINT('Ctrl Pts',(17.2887262067624,-16.8371668727754,
13.0903351641627));
#148266=CARTESIAN_POINT('Ctrl Pts',(17.3621717925896,-16.7888150309009,
13.0947216261752));
#148267=CARTESIAN_POINT('Ctrl Pts',(17.4377516489583,-16.7444356832877,
13.0991080881878));
#148268=CARTESIAN_POINT('Ctrl Pts',(17.5098539640989,-16.7020982952443,
13.1032927225808));
#148269=CARTESIAN_POINT('Ctrl Pts',(17.5841668423745,-16.6632182861073,
13.1074773569739));
#148270=CARTESIAN_POINT('Ctrl Pts',(17.6603248069611,-16.6280332231607,
13.1116619913669));
#148271=CARTESIAN_POINT('Ctrl Pts',(17.7363743701116,-16.5928982417961,
13.1158406694509));
#148272=CARTESIAN_POINT('Ctrl Pts',(17.8142633889644,-16.5614479512896,
13.1200193475348));
#148273=CARTESIAN_POINT('Ctrl Pts',(17.8935998508937,-16.5338751915209,
13.1241980256187));
#148274=CARTESIAN_POINT('Ctrl Pts',(17.9743583618848,-16.5058082098496,
13.1284516035042));
#148275=CARTESIAN_POINT('Ctrl Pts',(18.0566163014193,-16.4817593798135,
13.1327051813896));
#148276=CARTESIAN_POINT('Ctrl Pts',(18.1399366350505,-16.461881786255,13.136958759275));
#148277=CARTESIAN_POINT('Ctrl Pts',(18.221641641428,-16.4423895586354,13.141129873253));
#148278=CARTESIAN_POINT('Ctrl Pts',(18.3043677482547,-16.4269083873418,
13.145300987231));
#148279=CARTESIAN_POINT('Ctrl Pts',(18.3876870934188,-16.4155325015417,
13.1494721012089));
#148280=CARTESIAN_POINT('Ctrl Pts',(18.470978479972,-16.4041604330299,13.1536418155293));
#148281=CARTESIAN_POINT('Ctrl Pts',(18.5548622540878,-16.39689097632,13.1578115298496));
#148282=CARTESIAN_POINT('Ctrl Pts',(18.6389020976076,-16.3937669400618,
13.16198124417));
#148283=CARTESIAN_POINT('Ctrl Pts',(18.7229389506291,-16.3906430149703,
13.1661508101141));
#148284=CARTESIAN_POINT('Ctrl Pts',(18.8071314022655,-16.3916642332765,
13.1703203760581));
#148285=CARTESIAN_POINT('Ctrl Pts',(18.8910411442615,-16.3968213215102,
13.1744899420021));
#148286=CARTESIAN_POINT('Ctrl Pts',(18.9779010492722,-16.4021597266042,
13.1788061047411));
#148287=CARTESIAN_POINT('Ctrl Pts',(19.064457468181,-16.4119302148937,13.18312226748));
#148288=CARTESIAN_POINT('Ctrl Pts',(19.1502297723792,-16.4260639801085,
13.1874384302189));
#148289=CARTESIAN_POINT('Ctrl Pts',(19.2332080527898,-16.4397373394081,
13.1916139944106));
#148290=CARTESIAN_POINT('Ctrl Pts',(19.3154520685914,-16.4574939280207,
13.1957895586023));
#148291=CARTESIAN_POINT('Ctrl Pts',(19.3965387044157,-16.4792196892665,
13.1999651227939));
#148292=CARTESIAN_POINT('Ctrl Pts',(19.4817208334501,-16.5020427670648,
13.2043515848065));
#148293=CARTESIAN_POINT('Ctrl Pts',(19.5656250358877,-16.5292463408117,
13.208738046819));
#148294=CARTESIAN_POINT('Ctrl Pts',(19.6477828618953,-16.5606403697255,
13.2131245088315));
#148295=CARTESIAN_POINT('Ctrl Pts',(19.7299406879029,-16.5920343986394,
13.2175109708441));
#148296=CARTESIAN_POINT('Ctrl Pts',(19.8103516376767,-16.6276185783624,
13.2218974328566));
#148297=CARTESIAN_POINT('Ctrl Pts',(19.888577588602,-16.6671475776545,13.2262838948691));
#148298=CARTESIAN_POINT('Ctrl Pts',(19.9632042475667,-16.7048577890932,
13.2304685292622));
#148299=CARTESIAN_POINT('Ctrl Pts',(20.0361203339114,-16.7462981479268,
13.2346531636552));
#148300=CARTESIAN_POINT('Ctrl Pts',(20.1069282654733,-16.7912899366494,
13.2388377980483));
#148301=CARTESIAN_POINT('Ctrl Pts',(20.1776354107088,-16.8362176851296,
13.2430164761322));
#148302=CARTESIAN_POINT('Ctrl Pts',(20.2462399765314,-16.884686578031,13.2471951542162));
#148303=CARTESIAN_POINT('Ctrl Pts',(20.3123676261203,-16.9364713753421,
13.2513738323001));
#148304=CARTESIAN_POINT('Ctrl Pts',(20.379680566303,-16.9891843779279,13.2556274101855));
#148305=CARTESIAN_POINT('Ctrl Pts',(20.4444264890784,-17.0453331118989,
13.259880988071));
#148306=CARTESIAN_POINT('Ctrl Pts',(20.5062401158633,-17.1046329623692,
13.2641345659564));
#148307=CARTESIAN_POINT('Ctrl Pts',(20.5668553648736,-17.162783169524,13.2683056799344));
#148308=CARTESIAN_POINT('Ctrl Pts',(20.6246506525836,-17.2239630692774,
13.2724767939123));
#148309=CARTESIAN_POINT('Ctrl Pts',(20.6793151535296,-17.2878639017652,
13.2766479078903));
#148310=CARTESIAN_POINT('Ctrl Pts',(20.7339613112743,-17.3517432917116,
13.2808176222106));
#148311=CARTESIAN_POINT('Ctrl Pts',(20.7854784698982,-17.418341451807,13.284987336531));
#148312=CARTESIAN_POINT('Ctrl Pts',(20.8335944633575,-17.487314679039,13.2891570508514));
#148313=CARTESIAN_POINT('Ctrl Pts',(20.8817087446432,-17.5562854519076,
13.2933266167954));
#148314=CARTESIAN_POINT('Ctrl Pts',(20.9264218388937,-17.6276307460897,
13.2974961827395));
#148315=CARTESIAN_POINT('Ctrl Pts',(20.9675042956845,-17.7009769941527,
13.3016657486835));
#148316=CARTESIAN_POINT('Ctrl Pts',(21.0100311609753,-17.7769020058154,
13.3059819114224));
#148317=CARTESIAN_POINT('Ctrl Pts',(21.0486670744203,-17.8549708362667,
13.3102980741614));
#148318=CARTESIAN_POINT('Ctrl Pts',(21.0832097360536,-17.9347421093788,
13.3146142369003));
#148319=CARTESIAN_POINT('Ctrl Pts',(21.1166271741174,-18.0119148416597,
13.318789801092));
#148320=CARTESIAN_POINT('Ctrl Pts',(21.1462138190076,-18.0906803481868,
13.3229653652836));
#148321=CARTESIAN_POINT('Ctrl Pts',(21.1718365500182,-18.1706211191774,
13.3271409294753));
#148322=CARTESIAN_POINT('Ctrl Pts',(21.1987534242598,-18.2545995084698,
13.3315273914879));
#148323=CARTESIAN_POINT('Ctrl Pts',(21.2212952772081,-18.3398744431048,
13.3359138535004));
#148324=CARTESIAN_POINT('Ctrl Pts',(21.2393683400758,-18.4259491654358,
13.340300315513));
#148325=CARTESIAN_POINT('Ctrl Pts',(21.2574414029436,-18.5120238877669,
13.3446867775255));
#148326=CARTESIAN_POINT('Ctrl Pts',(21.2710456611134,-18.5988978127949,
13.349073239538));
#148327=CARTESIAN_POINT('Ctrl Pts',(21.2801502518719,-18.6860697555883,
13.3534597015506));
#148328=CARTESIAN_POINT('Ctrl Pts',(21.2888359269133,-18.7692307880738,
13.3576443359436));
#148329=CARTESIAN_POINT('Ctrl Pts',(21.2934592377886,-18.852972557727,13.3618289703367));
#148330=CARTESIAN_POINT('Ctrl Pts',(21.2939552539536,-18.9368640244713,
13.3660136047297));
#148331=CARTESIAN_POINT('Ctrl Pts',(21.294450564101,-19.0206360820962,13.3701922828137));
#148332=CARTESIAN_POINT('Ctrl Pts',(21.2908302458307,-19.1045569574875,
13.3743709608976));
#148333=CARTESIAN_POINT('Ctrl Pts',(21.2830810689264,-19.1881899744725,
13.3785496389816));
#148334=CARTESIAN_POINT('Ctrl Pts',(21.2751929935952,-19.2733220531809,
13.382803216867));
#148335=CARTESIAN_POINT('Ctrl Pts',(21.2630265340501,-19.3581553727241,
13.3870567947524));
#148336=CARTESIAN_POINT('Ctrl Pts',(21.2466232879999,-19.4422287349806,
13.3913103726379));
#148337=CARTESIAN_POINT('Ctrl Pts',(21.2305380508826,-19.5246721710542,
13.3954814866158));
#148338=CARTESIAN_POINT('Ctrl Pts',(21.2103789301821,-19.6063843810838,
13.3996526005938));
#148339=CARTESIAN_POINT('Ctrl Pts',(21.1862373001536,-19.6869368841851,
13.4038237145717));
#148340=CARTESIAN_POINT('Ctrl Pts',(21.1621037710821,-19.767462357116,13.4079934288921));
#148341=CARTESIAN_POINT('Ctrl Pts',(21.133990518692,-19.8468284556773,13.4121631432125));
#148342=CARTESIAN_POINT('Ctrl Pts',(21.1020392245072,-19.9246202913755,
13.4163328575329));
#148343=CARTESIAN_POINT('Ctrl Pts',(21.0700890672866,-20.0024093589063,
13.4205024234769));
#148344=CARTESIAN_POINT('Ctrl Pts',(21.0343013153838,-20.0786238497406,
13.4246719894209));
#148345=CARTESIAN_POINT('Ctrl Pts',(20.9948658827286,-20.1528686274168,
13.428841555365));
#148346=CARTESIAN_POINT('Ctrl Pts',(20.9540439489101,-20.2297237598852,
13.4331577181039));
#148347=CARTESIAN_POINT('Ctrl Pts',(20.9093133043205,-20.3044676260572,
13.4374738808428));
#148348=CARTESIAN_POINT('Ctrl Pts',(20.8609355752996,-20.3766912151498,
13.4417900435818));
#148349=CARTESIAN_POINT('Ctrl Pts',(20.8141337457131,-20.4465621284243,
13.4459656077734));
#148350=CARTESIAN_POINT('Ctrl Pts',(20.7639191093593,-20.5140740893661,
13.4501411719651));
#148351=CARTESIAN_POINT('Ctrl Pts',(20.7105706701799,-20.5788891744014,
13.4543167361568));
#148352=CARTESIAN_POINT('Ctrl Pts',(20.6545277281615,-20.6469779152986,
13.4587031981693));
#148353=CARTESIAN_POINT('Ctrl Pts',(20.5950264806454,-20.7120897510532,
13.4630896601819));
#148354=CARTESIAN_POINT('Ctrl Pts',(20.5324338669328,-20.7738769514622,
13.4674761221944));
#148355=CARTESIAN_POINT('Ctrl Pts',(20.4698412532202,-20.8356641518712,
13.4718625842069));
#148356=CARTESIAN_POINT('Ctrl Pts',(20.4041577572905,-20.8941263879947,
13.4762490462195));
#148357=CARTESIAN_POINT('Ctrl Pts',(20.3357880909558,-20.9489664272771,
13.480635508232));
#148358=CARTESIAN_POINT('Ctrl Pts',(20.3218259558186,-20.9601656049306,
13.4815312910942));
#148359=CARTESIAN_POINT('Ctrl Pts',(20.3077408189587,-20.9712227949802,
13.4824270739563));
#148360=CARTESIAN_POINT('Ctrl Pts',(20.2935357468249,-20.9821350335323,
13.4833228568185));
#148361=CARTESIAN_POINT('Origin',(18.734,-18.952,-1.76670989022851));
#148362=CARTESIAN_POINT('',(20.2947698132858,-20.9837129250579,14.3497865232697));
#148363=CARTESIAN_POINT('',(20.2923704978255,-20.9805871927216,14.2834124327049));
#148364=CARTESIAN_POINT('',(20.2935357468249,-20.9821350335323,-1.76670989022851));
#148365=CARTESIAN_POINT('',(16.1740010575059,-18.949673107456,13.8332901097715));
#148366=CARTESIAN_POINT('Ctrl Pts',(16.1735504202813,-18.9496726978525,
13.8332901097715));
#148367=CARTESIAN_POINT('Ctrl Pts',(16.1718449019213,-18.765781352641,13.8424428639771));
#148368=CARTESIAN_POINT('Ctrl Pts',(16.2739023737919,-17.7320561796712,
13.8939875537431));
#148369=CARTESIAN_POINT('Ctrl Pts',(17.6781137265109,-16.1150307104843,
13.9879241790696));
#148370=CARTESIAN_POINT('Ctrl Pts',(20.5479109989865,-16.5285690725847,
14.1150999857511));
#148371=CARTESIAN_POINT('Ctrl Pts',(21.6914148502026,-19.029541834012,14.2357207671511));
#148372=CARTESIAN_POINT('Ctrl Pts',(20.8607340421186,-20.5404053550185,
14.3139496129906));
#148373=CARTESIAN_POINT('Ctrl Pts',(20.2947698132858,-20.9837129250579,
14.3497865232697));
#148374=CARTESIAN_POINT('Ctrl Pts',(20.2935357468249,-20.9821350335323,
13.5498657043958));
#148375=CARTESIAN_POINT('Ctrl Pts',(20.2268456522252,-21.0333659047647,
13.5540358081023));
#148376=CARTESIAN_POINT('Ctrl Pts',(20.157642311523,-21.0812965736288,13.5582059118088));
#148377=CARTESIAN_POINT('Ctrl Pts',(20.0862913281455,-21.125685387498,13.5623760155153));
#148378=CARTESIAN_POINT('Ctrl Pts',(20.014862529641,-21.1701226116488,13.566550667122));
#148379=CARTESIAN_POINT('Ctrl Pts',(19.9412818046901,-21.2110100274126,
13.5707253187287));
#148380=CARTESIAN_POINT('Ctrl Pts',(19.8659411674346,-21.2481509518032,
13.5748999703354));
#148381=CARTESIAN_POINT('Ctrl Pts',(19.7905547245971,-21.2853144571238,
13.5790771600457));
#148382=CARTESIAN_POINT('Ctrl Pts',(19.7134066615509,-21.3187267542991,
13.583254349756));
#148383=CARTESIAN_POINT('Ctrl Pts',(19.6349086504671,-21.3482394712369,
13.5874315394664));
#148384=CARTESIAN_POINT('Ctrl Pts',(19.5562800787177,-21.3778012747683,
13.5916156768262));
#148385=CARTESIAN_POINT('Ctrl Pts',(19.4762975144192,-21.4034504101753,
13.595799814186));
#148386=CARTESIAN_POINT('Ctrl Pts',(19.3953870533626,-21.4250885883131,
13.5999839515459));
#148387=CARTESIAN_POINT('Ctrl Pts',(19.3540513159326,-21.4361431545371,
13.6021215540391));
#148388=CARTESIAN_POINT('Ctrl Pts',(19.3124735532324,-21.4461516842229,
13.6042591565322));
#148389=CARTESIAN_POINT('Ctrl Pts',(19.2707112385803,-21.4551062794819,
13.6063967590254));
#148390=CARTESIAN_POINT('Ctrl Pts',(19.1889560858866,-21.4726360622251,
13.6105813934184));
#148391=CARTESIAN_POINT('Ctrl Pts',(19.1061890642126,-21.486188888916,13.6147660278115));
#148392=CARTESIAN_POINT('Ctrl Pts',(19.022831797239,-21.4956541024486,13.6189506622045));
#148393=CARTESIAN_POINT('Ctrl Pts',(18.9395931790174,-21.5051058434214,
13.6231293402885));
#148394=CARTESIAN_POINT('Ctrl Pts',(18.8557664374669,-21.5104814765754,
13.6273080183724));
#148395=CARTESIAN_POINT('Ctrl Pts',(18.7717843292961,-21.5117211458398,
13.6314866964563));
#148396=CARTESIAN_POINT('Ctrl Pts',(18.6862969021932,-21.5129830352849,
13.6357402743418));
#148397=CARTESIAN_POINT('Ctrl Pts',(18.6006489552156,-21.5099591270341,
13.6399938522272));
#148398=CARTESIAN_POINT('Ctrl Pts',(18.5153034901263,-21.5026414559026,
13.6442474301127));
#148399=CARTESIAN_POINT('Ctrl Pts',(18.4316126134156,-21.4954656521053,
13.6484185440906));
#148400=CARTESIAN_POINT('Ctrl Pts',(18.3482130743118,-21.4841611267896,
13.6525896580686));
#148401=CARTESIAN_POINT('Ctrl Pts',(18.2655406684998,-21.4687729048785,
13.6567607720465));
#148402=CARTESIAN_POINT('Ctrl Pts',(18.1828960042121,-21.4533898466338,
13.6609304863669));
#148403=CARTESIAN_POINT('Ctrl Pts',(18.1009784405236,-21.4339258973909,
13.6651002006873));
#148404=CARTESIAN_POINT('Ctrl Pts',(18.0202156389588,-21.4104775544904,
13.6692699150076));
#148405=CARTESIAN_POINT('Ctrl Pts',(17.939455711281,-21.3870300459826,13.6734394809517));
#148406=CARTESIAN_POINT('Ctrl Pts',(17.8598509055783,-21.3595985548016,
13.6776090468957));
#148407=CARTESIAN_POINT('Ctrl Pts',(17.7818144029985,-21.3283296465059,
13.6817786128398));
#148408=CARTESIAN_POINT('Ctrl Pts',(17.7010342332564,-21.2959613619689,
13.6860947755787));
#148409=CARTESIAN_POINT('Ctrl Pts',(17.6219351912173,-21.2594809885574,
13.6904109383176));
#148410=CARTESIAN_POINT('Ctrl Pts',(17.5449519222896,-21.2191049091062,
13.6947271010565));
#148411=CARTESIAN_POINT('Ctrl Pts',(17.4704763752501,-21.1800440761963,
13.6989026652482));
#148412=CARTESIAN_POINT('Ctrl Pts',(17.3979812574152,-21.1373377246259,
13.7030782294399));
#148413=CARTESIAN_POINT('Ctrl Pts',(17.3278323932016,-21.091227117814,13.7072537936316));
#148414=CARTESIAN_POINT('Ctrl Pts',(17.2541404766197,-21.0427875738696,
13.7116402556441));
#148415=CARTESIAN_POINT('Ctrl Pts',(17.1830385318335,-20.9905911845411,
13.7160267176566));
#148416=CARTESIAN_POINT('Ctrl Pts',(17.1149115381732,-20.9349655954603,
13.7204131796692));
#148417=CARTESIAN_POINT('Ctrl Pts',(17.0467845445129,-20.8793400063795,
13.7247996416817));
#148418=CARTESIAN_POINT('Ctrl Pts',(16.9816328807925,-20.8202856635707,
13.7291861036943));
#148419=CARTESIAN_POINT('Ctrl Pts',(16.9197953580219,-20.7581731691688,
13.7335725657068));
#148420=CARTESIAN_POINT('Ctrl Pts',(16.8612222805613,-20.6993396360182,
13.7377274633762));
#148421=CARTESIAN_POINT('Ctrl Pts',(16.8053896617352,-20.6375286216453,
13.7418823610455));
#148422=CARTESIAN_POINT('Ctrl Pts',(16.7526212754374,-20.5730300274365,
13.7460372587149));
#148423=CARTESIAN_POINT('Ctrl Pts',(16.7002946208399,-20.5090713601742,
13.7501573751423));
#148424=CARTESIAN_POINT('Ctrl Pts',(16.6509814300939,-20.4424702805592,
13.7542774915697));
#148425=CARTESIAN_POINT('Ctrl Pts',(16.6049624110076,-20.3735480803186,
13.7583976079971));
#148426=CARTESIAN_POINT('Ctrl Pts',(16.5589874739682,-20.3046919012954,
13.7625137777266));
#148427=CARTESIAN_POINT('Ctrl Pts',(16.5163007099123,-20.2335194044224,
13.7666299474561));
#148428=CARTESIAN_POINT('Ctrl Pts',(16.4771421768208,-20.1603843618463,
13.7707461171856));
#148429=CARTESIAN_POINT('Ctrl Pts',(16.4380086398887,-20.0872960037358,
13.7748596594307));
#148430=CARTESIAN_POINT('Ctrl Pts',(16.4023990866291,-20.0122480031431,
13.7789732016757));
#148431=CARTESIAN_POINT('Ctrl Pts',(16.3705090605919,-19.9356211564092,
13.7830867439208));
#148432=CARTESIAN_POINT('Ctrl Pts',(16.3380758082443,-19.8576890200784,
13.7872703577417));
#148433=CARTESIAN_POINT('Ctrl Pts',(16.3094902338592,-19.7781241832446,
13.7914539715626));
#148434=CARTESIAN_POINT('Ctrl Pts',(16.2849076425233,-19.6973500013747,
13.7956375853835));
#148435=CARTESIAN_POINT('Ctrl Pts',(16.2607361379239,-19.6179265800639,
13.7997512379815));
#148436=CARTESIAN_POINT('Ctrl Pts',(16.2404348481341,-19.5373344318006,
13.8038648905795));
#148437=CARTESIAN_POINT('Ctrl Pts',(16.2241009663662,-19.455990913573,13.8079785431774));
#148438=CARTESIAN_POINT('Ctrl Pts',(16.2073503971231,-19.3725722716413,
13.8121971376098));
#148439=CARTESIAN_POINT('Ctrl Pts',(16.1947725425284,-19.2883639128979,
13.8164157320421));
#148440=CARTESIAN_POINT('Ctrl Pts',(16.1864159534739,-19.2038243949375,
13.8206343264745));
#148441=CARTESIAN_POINT('Ctrl Pts',(16.1780593644194,-19.1192848769771,
13.8248529209068));
#148442=CARTESIAN_POINT('Ctrl Pts',(16.1739240322153,-19.0344147354448,
13.8290715153392));
#148443=CARTESIAN_POINT('Ctrl Pts',(16.1740010575059,-18.949673107456,13.8332901097715));
#148444=CARTESIAN_POINT('',(16.1740010826188,-18.9543543591274,13.7667098774921));
#148445=CARTESIAN_POINT('Ctrl Pts',(20.2935357468249,-20.9821350335323,
13.4833228568185));
#148446=CARTESIAN_POINT('Ctrl Pts',(20.2271990631406,-21.0330944169343,
13.4875060995234));
#148447=CARTESIAN_POINT('Ctrl Pts',(20.1582439358111,-21.0808896740306,
13.4916893422283));
#148448=CARTESIAN_POINT('Ctrl Pts',(20.0870050715129,-21.1252411915064,
13.4958725849332));
#148449=CARTESIAN_POINT('Ctrl Pts',(20.0158625563524,-21.1695327244428,
13.5000501698861));
#148450=CARTESIAN_POINT('Ctrl Pts',(19.942442827238,-21.2103895284926,13.504227754839));
#148451=CARTESIAN_POINT('Ctrl Pts',(19.8671122352966,-21.247573275289,13.5084053397919));
#148452=CARTESIAN_POINT('Ctrl Pts',(19.7918615905526,-21.2847175595474,
13.5125784911382));
#148453=CARTESIAN_POINT('Ctrl Pts',(19.7147045242392,-21.3181963316418,
13.5167516424845));
#148454=CARTESIAN_POINT('Ctrl Pts',(19.6360336482658,-21.3478162069317,
13.5209247938308));
#148455=CARTESIAN_POINT('Ctrl Pts',(19.5574081725827,-21.3774189888445,
13.5250955368872));
#148456=CARTESIAN_POINT('Ctrl Pts',(19.4772710512136,-21.4031671335675,
13.5292662799435));
#148457=CARTESIAN_POINT('Ctrl Pts',(19.3960355903709,-21.4249150565845,
13.5334370229998));
#148458=CARTESIAN_POINT('Ctrl Pts',(19.3148226408376,-21.4466569529941,
13.5376066102938));
#148459=CARTESIAN_POINT('Ctrl Pts',(19.2325124005023,-21.4644007105937,
13.5417761975877));
#148460=CARTESIAN_POINT('Ctrl Pts',(19.1495327658116,-21.4780507755263,
13.5459457848817));
#148461=CARTESIAN_POINT('Ctrl Pts',(19.0665512339994,-21.4917011525335,
13.5501154675029));
#148462=CARTESIAN_POINT('Ctrl Pts',(18.982900731597,-21.5012575776353,13.554285150124));
#148463=CARTESIAN_POINT('Ctrl Pts',(18.8990174051097,-21.5066759591014,
13.5584548327451));
#148464=CARTESIAN_POINT('Ctrl Pts',(18.8150490006465,-21.5120998361166,
13.5626287444327));
#148465=CARTESIAN_POINT('Ctrl Pts',(18.7308477605494,-21.5133772563818,
13.5668026561202));
#148466=CARTESIAN_POINT('Ctrl Pts',(18.6468525185955,-21.5105162333831,
13.5709765678078));
#148467=CARTESIAN_POINT('Ctrl Pts',(18.5628158450396,-21.5076537991525,
13.5751525383244));
#148468=CARTESIAN_POINT('Ctrl Pts',(18.4789858309805,-21.5006488937704,
13.579328508841));
#148469=CARTESIAN_POINT('Ctrl Pts',(18.3957964105736,-21.4895614932646,
13.5835044793576));
#148470=CARTESIAN_POINT('Ctrl Pts',(18.312457595632,-21.4784541816086,13.5876879492314));
#148471=CARTESIAN_POINT('Ctrl Pts',(18.2297621264903,-21.4632498088279,
13.5918714191051));
#148472=CARTESIAN_POINT('Ctrl Pts',(18.1481338832284,-21.4440595685535,
13.5960548889789));
#148473=CARTESIAN_POINT('Ctrl Pts',(18.0716697338467,-21.4260833713406,
13.5999736976237));
#148474=CARTESIAN_POINT('Ctrl Pts',(17.9961422166987,-21.4046102585772,
13.6038925062686));
#148475=CARTESIAN_POINT('Ctrl Pts',(17.921884774769,-21.379770347654,13.6078113149135));
#148476=CARTESIAN_POINT('Ctrl Pts',(17.842590205016,-21.353245463438,13.6119959493065));
#148477=CARTESIAN_POINT('Ctrl Pts',(17.7644489508446,-21.3227823154618,
13.6161805836996));
#148478=CARTESIAN_POINT('Ctrl Pts',(17.6878802554244,-21.2885002632162,
13.6203652180926));
#148479=CARTESIAN_POINT('Ctrl Pts',(17.6114205460648,-21.2542670072286,
13.6245438961766));
#148480=CARTESIAN_POINT('Ctrl Pts',(17.5365293656821,-21.2162258304372,
13.6287225742605));
#148481=CARTESIAN_POINT('Ctrl Pts',(17.4636096823068,-21.1745454867587,
13.6329012523444));
#148482=CARTESIAN_POINT('Ctrl Pts',(17.3893829660135,-21.1321180528749,
13.6371548302299));
#148483=CARTESIAN_POINT('Ctrl Pts',(17.3171995773183,-21.0859198576824,
13.6414084081153));
#148484=CARTESIAN_POINT('Ctrl Pts',(17.2474621052953,-21.0361797157651,
13.6456619860008));
#148485=CARTESIAN_POINT('Ctrl Pts',(17.1790766302489,-20.9874038835589,
13.6498330999787));
#148486=CARTESIAN_POINT('Ctrl Pts',(17.1130434722312,-20.9352224936048,
13.6540042139567));
#148487=CARTESIAN_POINT('Ctrl Pts',(17.0497148300457,-20.879896124347,13.6581753279346));
#148488=CARTESIAN_POINT('Ctrl Pts',(16.9864074383977,-20.8245883203866,
13.662345042255));
#148489=CARTESIAN_POINT('Ctrl Pts',(16.9258031063752,-20.7661379354358,
13.6665147565754));
#148490=CARTESIAN_POINT('Ctrl Pts',(16.8682208314237,-20.7048457131495,
13.6706844708957));
#148491=CARTESIAN_POINT('Ctrl Pts',(16.8106406054966,-20.6435556719036,
13.6748540368398));
#148492=CARTESIAN_POINT('Ctrl Pts',(16.7560825371937,-20.5794243302491,
13.6790236027838));
#148493=CARTESIAN_POINT('Ctrl Pts',(16.7048276747609,-20.512788158106,13.6831931687279));
#148494=CARTESIAN_POINT('Ctrl Pts',(16.6517707545947,-20.4438091403549,
13.6875093314668));
#148495=CARTESIAN_POINT('Ctrl Pts',(16.6022539651132,-20.3721462932498,
13.6918254942057));
#148496=CARTESIAN_POINT('Ctrl Pts',(16.5565412927829,-20.2982071082729,
13.6961416569446));
#148497=CARTESIAN_POINT('Ctrl Pts',(16.5123177059456,-20.2266764844696,
13.7003172211363));
#148498=CARTESIAN_POINT('Ctrl Pts',(16.4716543903427,-20.1530159839383,
13.704492785328));
#148499=CARTESIAN_POINT('Ctrl Pts',(16.4347434295141,-20.0776194841408,
13.7086683495197));
#148500=CARTESIAN_POINT('Ctrl Pts',(16.3959681838015,-19.9984148863766,
13.7130548115322));
#148501=CARTESIAN_POINT('Ctrl Pts',(16.3613345469612,-19.9172948468639,
13.7174412735447));
#148502=CARTESIAN_POINT('Ctrl Pts',(16.3310071212994,-19.8347373476376,
13.7218277355573));
#148503=CARTESIAN_POINT('Ctrl Pts',(16.3006796956376,-19.7521798484113,
13.7262141975698));
#148504=CARTESIAN_POINT('Ctrl Pts',(16.2746585801944,-19.668185466211,13.7306006595824));
#148505=CARTESIAN_POINT('Ctrl Pts',(16.253046772176,-19.5832456584798,13.7349871215949));
#148506=CARTESIAN_POINT('Ctrl Pts',(16.2263033450823,-19.4781373050522,
13.7404151277539));
#148507=CARTESIAN_POINT('Ctrl Pts',(16.2062281520528,-19.3712684537335,
13.745843133913));
#148508=CARTESIAN_POINT('Ctrl Pts',(16.193006541868,-19.2633715557504,13.751271140072));
#148509=CARTESIAN_POINT('Ctrl Pts',(16.1804712473274,-19.161075437704,13.7564173858787));
#148510=CARTESIAN_POINT('Ctrl Pts',(16.1740962693079,-19.0578550605845,
13.7615636316854));
#148511=CARTESIAN_POINT('Ctrl Pts',(16.1740010826188,-18.9543543591274,
13.7667098774921));
#148512=CARTESIAN_POINT('Ctrl Pts',(16.1744182719781,-18.9543537193378,
13.7667098902285));
#148513=CARTESIAN_POINT('Ctrl Pts',(16.1802301241212,-18.3145386211268,
13.7985275695778));
#148514=CARTESIAN_POINT('Ctrl Pts',(16.7471749526305,-16.8130883553205,
13.8727371844876));
#148515=CARTESIAN_POINT('Ctrl Pts',(19.2691669536258,-15.9725892909193,
13.9893387349578));
#148516=CARTESIAN_POINT('Ctrl Pts',(21.5288886261234,-17.7892922081608,
14.1165145416392));
#148517=CARTESIAN_POINT('Ctrl Pts',(21.2942515057879,-20.0117708843731,
14.2145391075549));
#148518=CARTESIAN_POINT('Ctrl Pts',(20.505242856169,-20.8199787376498,14.2701717379101));
#148519=CARTESIAN_POINT('Ctrl Pts',(20.2923704978253,-20.9805871927218,
14.2834124327049));
#148520=CARTESIAN_POINT('Origin',(18.734,-18.952,-1.76670989022851));
#148521=CARTESIAN_POINT('',(20.2935357468249,-20.9821350335323,15.1499553861536));
#148522=CARTESIAN_POINT('',(20.2935357468249,-20.9821350335323,15.0832685855196));
#148523=CARTESIAN_POINT('',(20.2935357468249,-20.9821350335323,-1.76670989022851));
#148524=CARTESIAN_POINT('',(16.1738766836434,-18.9531301832654,14.6332901097715));
#148525=CARTESIAN_POINT('Ctrl Pts',(16.1740002494514,-18.9531301287164,
14.6332901097715));
#148526=CARTESIAN_POINT('Ctrl Pts',(16.1739637014967,-18.8703406609987,
14.6374299052976));
#148527=CARTESIAN_POINT('Ctrl Pts',(16.1779474618949,-18.787387492894,14.6415697008237));
#148528=CARTESIAN_POINT('Ctrl Pts',(16.1859729132155,-18.7046986352396,
14.6457094963498));
#148529=CARTESIAN_POINT('Ctrl Pts',(16.1939875490477,-18.6221212131097,
14.6498437128863));
#148530=CARTESIAN_POINT('Ctrl Pts',(16.2060330170348,-18.5398078587028,
14.6539779294227));
#148531=CARTESIAN_POINT('Ctrl Pts',(16.2220786798974,-18.4581869973217,
14.6581121459591));
#148532=CARTESIAN_POINT('Ctrl Pts',(16.2381078732803,-18.3766499126678,
14.6622421190812));
#148533=CARTESIAN_POINT('Ctrl Pts',(16.2581290152451,-18.2958043686403,
14.6663720922033));
#148534=CARTESIAN_POINT('Ctrl Pts',(16.2820597821146,-18.2160725797227,
14.6705020653254));
#148535=CARTESIAN_POINT('Ctrl Pts',(16.3059775967093,-18.1363839447938,
14.6746298031431));
#148536=CARTESIAN_POINT('Ctrl Pts',(16.3338007023324,-18.0578083185529,
14.6787575409609));
#148537=CARTESIAN_POINT('Ctrl Pts',(16.3653962152435,-17.9807553805363,
14.6828852787787));
#148538=CARTESIAN_POINT('Ctrl Pts',(16.3969845852848,-17.9037198620533,
14.6870120834293));
#148539=CARTESIAN_POINT('Ctrl Pts',(16.4323434905918,-17.8282067834232,
14.69113888808));
#148540=CARTESIAN_POINT('Ctrl Pts',(16.4712914723378,-17.7546069488907,
14.6952656927306));
#148541=CARTESIAN_POINT('Ctrl Pts',(16.510242924153,-17.6810005569833,14.6993928650588));
#148542=CARTESIAN_POINT('Ctrl Pts',(16.5527838651356,-17.609308162424,14.703520037387));
#148543=CARTESIAN_POINT('Ctrl Pts',(16.5986870593953,-17.5398956675635,
14.7076472097152));
#148544=CARTESIAN_POINT('Ctrl Pts',(16.6446377721095,-17.4704113176929,
14.7117786544443));
#148545=CARTESIAN_POINT('Ctrl Pts',(16.6939574240315,-17.4032119705958,
14.7159100991734));
#148546=CARTESIAN_POINT('Ctrl Pts',(16.746376041612,-17.3386336435756,14.7200415439026));
#148547=CARTESIAN_POINT('Ctrl Pts',(16.7988250781874,-17.2740178411719,
14.7241753861462));
#148548=CARTESIAN_POINT('Ctrl Pts',(16.8543763437697,-17.2120264344659,
14.7283092283899));
#148549=CARTESIAN_POINT('Ctrl Pts',(16.9127219511753,-17.1529596255589,
14.7324430706335));
#148550=CARTESIAN_POINT('Ctrl Pts',(16.9711635405876,-17.0937956482256,
14.7365837132944));
#148551=CARTESIAN_POINT('Ctrl Pts',(17.0324082986517,-17.0375661867597,
14.7407243559553));
#148552=CARTESIAN_POINT('Ctrl Pts',(17.0961145829386,-16.9845317383557,
14.7448649986161));
#148553=CARTESIAN_POINT('Ctrl Pts',(17.1274705472736,-16.9584284066154,
14.7469030054635));
#148554=CARTESIAN_POINT('Ctrl Pts',(17.1594223751532,-16.9330984310461,
14.7489410123109));
#148555=CARTESIAN_POINT('Ctrl Pts',(17.1919269101816,-16.9085689182999,
14.7509790191583));
#148556=CARTESIAN_POINT('Ctrl Pts',(17.2586683911458,-16.8582025307613,
14.7551636535514));
#148557=CARTESIAN_POINT('Ctrl Pts',(17.3280042311001,-16.8110156651531,
14.7593482879444));
#148558=CARTESIAN_POINT('Ctrl Pts',(17.3995987737075,-16.767286433587,14.7635329223375));
#148559=CARTESIAN_POINT('Ctrl Pts',(17.4710914103451,-16.7236194451695,
14.7677116004214));
#148560=CARTESIAN_POINT('Ctrl Pts',(17.5448359744308,-16.6834005528598,
14.7718902785053));
#148561=CARTESIAN_POINT('Ctrl Pts',(17.6204652949934,-16.6468664982813,
14.7760689565893));
#148562=CARTESIAN_POINT('Ctrl Pts',(17.6974502167732,-16.6096775970311,
14.7803225344747));
#148563=CARTESIAN_POINT('Ctrl Pts',(17.7763877432994,-16.5763072247155,
14.7845761123602));
#148564=CARTESIAN_POINT('Ctrl Pts',(17.8568613993349,-16.5469578225687,
14.7888296902456));
#148565=CARTESIAN_POINT('Ctrl Pts',(17.9357749165169,-16.5181774158532,
14.7930008042235));
#148566=CARTESIAN_POINT('Ctrl Pts',(18.0161650809,-16.4932636267837,14.7971719182015));
#148567=CARTESIAN_POINT('Ctrl Pts',(18.0976177441666,-16.4723593759457,
14.8013430321794));
#148568=CARTESIAN_POINT('Ctrl Pts',(18.1790430752053,-16.451462139731,14.8055127464998));
#148569=CARTESIAN_POINT('Ctrl Pts',(18.2615297518284,-16.434571883947,14.8096824608202));
#148570=CARTESIAN_POINT('Ctrl Pts',(18.3446492988108,-16.4217814261445,
14.8138521751405));
#148571=CARTESIAN_POINT('Ctrl Pts',(18.4277658880431,-16.4089914234813,
14.8180217410846));
#148572=CARTESIAN_POINT('Ctrl Pts',(18.5115148480479,-16.4003009978601,
14.8221913070286));
#148573=CARTESIAN_POINT('Ctrl Pts',(18.5954597232801,-16.3957514612764,
14.8263608729727));
#148574=CARTESIAN_POINT('Ctrl Pts',(18.6823559967683,-16.3910419685989,
14.8306770357116));
#148575=CARTESIAN_POINT('Ctrl Pts',(18.7694616919212,-16.3907699986349,
14.8349931984505));
#148576=CARTESIAN_POINT('Ctrl Pts',(18.8562914526112,-16.3949226056652,
14.8393093611894));
#148577=CARTESIAN_POINT('Ctrl Pts',(18.9402927429795,-16.3989399419582,
14.8434849253811));
#148578=CARTESIAN_POINT('Ctrl Pts',(19.0240353356995,-16.4070979281598,
14.8476604895728));
#148579=CARTESIAN_POINT('Ctrl Pts',(19.1070857885139,-16.4193320402372,
14.8518360537645));
#148580=CARTESIAN_POINT('Ctrl Pts',(19.1943309222662,-16.4321840682319,
14.856222515777));
#148581=CARTESIAN_POINT('Ctrl Pts',(19.2808115861347,-16.4495346990029,
14.8606089777895));
#148582=CARTESIAN_POINT('Ctrl Pts',(19.3660405469235,-16.471249156597,14.8649954398021));
#148583=CARTESIAN_POINT('Ctrl Pts',(19.4512695077123,-16.4929636141912,
14.8693819018146));
#148584=CARTESIAN_POINT('Ctrl Pts',(19.5352462338659,-16.5190416538915,
14.8737683638271));
#148585=CARTESIAN_POINT('Ctrl Pts',(19.6175072439393,-16.549290082031,14.8781548258397));
#148586=CARTESIAN_POINT('Ctrl Pts',(19.6959833029992,-16.5781467351528,
14.8823394602327));
#148587=CARTESIAN_POINT('Ctrl Pts',(19.7731901646014,-16.6109058485357,
14.8865240946257));
#148588=CARTESIAN_POINT('Ctrl Pts',(19.848712296063,-16.6474357251303,14.8907087290188));
#148589=CARTESIAN_POINT('Ctrl Pts',(19.9241269311184,-16.683913605967,14.8948874071027));
#148590=CARTESIAN_POINT('Ctrl Pts',(19.9978611886366,-16.7241513904372,
14.8990660851867));
#148591=CARTESIAN_POINT('Ctrl Pts',(20.0695172636948,-16.7679684896108,
14.9032447632706));
#148592=CARTESIAN_POINT('Ctrl Pts',(20.1424577224,-16.8125709787961,14.9074983411561));
#148593=CARTESIAN_POINT('Ctrl Pts',(20.2132443104816,-16.860882196855,14.9117519190415));
#148594=CARTESIAN_POINT('Ctrl Pts',(20.281481376752,-16.9126615316221,14.9160054969269));
#148595=CARTESIAN_POINT('Ctrl Pts',(20.3483955343389,-16.9634370229456,
14.9201766109049));
#148596=CARTESIAN_POINT('Ctrl Pts',(20.4128577595142,-17.0175470676764,
14.9243477248828));
#148597=CARTESIAN_POINT('Ctrl Pts',(20.4745237080537,-17.074720792822,14.9285188388608));
#148598=CARTESIAN_POINT('Ctrl Pts',(20.5361689639887,-17.1318753327719,
14.9326885531812));
#148599=CARTESIAN_POINT('Ctrl Pts',(20.5950194697347,-17.1920911989055,
14.9368582675015));
#148600=CARTESIAN_POINT('Ctrl Pts',(20.6507652549076,-17.2550583517459,
14.9410279818219));
#148601=CARTESIAN_POINT('Ctrl Pts',(20.7065090564062,-17.3180232639449,
14.9451975477659));
#148602=CARTESIAN_POINT('Ctrl Pts',(20.75914805269,-17.3837389231869,14.94936711371));
#148603=CARTESIAN_POINT('Ctrl Pts',(20.8084112617999,-17.4518607008288,
14.953536679654));
#148604=CARTESIAN_POINT('Ctrl Pts',(20.8594065045693,-17.5223775561353,
14.957852842393));
#148605=CARTESIAN_POINT('Ctrl Pts',(20.9067838489651,-17.5954724488007,
14.9621690051319));
#148606=CARTESIAN_POINT('Ctrl Pts',(20.9502914662219,-17.6707302638585,
14.9664851678708));
#148607=CARTESIAN_POINT('Ctrl Pts',(20.9923818274227,-17.7435365635066,
14.9706607320625));
#148608=CARTESIAN_POINT('Ctrl Pts',(21.0308505291919,-17.8183665946339,
14.9748362962542));
#148609=CARTESIAN_POINT('Ctrl Pts',(21.0655172119571,-17.8948209752611,
14.9790118604458));
#148610=CARTESIAN_POINT('Ctrl Pts',(21.1019348264565,-17.9751368849007,
14.9833983224584));
#148611=CARTESIAN_POINT('Ctrl Pts',(21.1341560348915,-18.0572450047082,
14.9877847844709));
#148612=CARTESIAN_POINT('Ctrl Pts',(21.1620304324222,-18.1406626970047,
14.9921712464835));
#148613=CARTESIAN_POINT('Ctrl Pts',(21.1899048299529,-18.2240803893013,
14.996557708496));
#148614=CARTESIAN_POINT('Ctrl Pts',(21.2134323346265,-18.3088070746723,
15.0009441705086));
#148615=CARTESIAN_POINT('Ctrl Pts',(21.2325245180281,-18.3943484665022,
15.0053306325211));
#148616=CARTESIAN_POINT('Ctrl Pts',(21.25073824177,-18.4759539720913,15.0095152669141));
#148617=CARTESIAN_POINT('Ctrl Pts',(21.2649836214983,-18.5586046111965,
15.0136999013072));
#148618=CARTESIAN_POINT('Ctrl Pts',(21.2751464736302,-18.6418797014761,
15.0178845357002));
#148619=CARTESIAN_POINT('Ctrl Pts',(21.2852948602001,-18.725036259972,15.0220632137842));
#148620=CARTESIAN_POINT('Ctrl Pts',(21.2913722063418,-18.8088150514091,
15.0262418918681));
#148621=CARTESIAN_POINT('Ctrl Pts',(21.2933150345072,-18.8927838354387,
15.0304205699521));
#148622=CARTESIAN_POINT('Ctrl Pts',(21.2952926864712,-18.9782576995749,
15.0346741478375));
#148623=CARTESIAN_POINT('Ctrl Pts',(21.2929860350544,-19.0639279639717,
15.0389277257229));
#148624=CARTESIAN_POINT('Ctrl Pts',(21.2863832385264,-19.1493317097919,
15.0431813036084));
#148625=CARTESIAN_POINT('Ctrl Pts',(21.2799084500935,-19.2330797373477,
15.0473524175863));
#148626=CARTESIAN_POINT('Ctrl Pts',(21.2693026454397,-19.3165710082865,
15.0515235315643));
#148627=CARTESIAN_POINT('Ctrl Pts',(21.2546071988876,-19.3993693651963,
15.0556946455422));
#148628=CARTESIAN_POINT('Ctrl Pts',(21.2399166835345,-19.4821399383178,
15.0598643598626));
#148629=CARTESIAN_POINT('Ctrl Pts',(21.2211393320557,-19.5642176066098,
15.064034074183));
#148630=CARTESIAN_POINT('Ctrl Pts',(21.1983680574964,-19.6451739155445,
15.0682037885034));
#148631=CARTESIAN_POINT('Ctrl Pts',(21.1755975932368,-19.7261273437063,
15.0723733544474));
#148632=CARTESIAN_POINT('Ctrl Pts',(21.1488336138537,-19.8059590492309,
15.0765429203915));
#148633=CARTESIAN_POINT('Ctrl Pts',(21.1182192201024,-19.8842546382263,
15.0807124863355));
#148634=CARTESIAN_POINT('Ctrl Pts',(21.0865284620338,-19.9653030035426,
15.0850286490744));
#148635=CARTESIAN_POINT('Ctrl Pts',(21.0507116827588,-20.0447047315976,
15.0893448118133));
#148636=CARTESIAN_POINT('Ctrl Pts',(21.0109816181364,-20.1220233803941,
15.0936609745523));
#148637=CARTESIAN_POINT('Ctrl Pts',(20.9725457561902,-20.1968233823388,
15.0978365387439));
#148638=CARTESIAN_POINT('Ctrl Pts',(20.9304479207723,-20.2696735493081,
15.1020121029356));
#148639=CARTESIAN_POINT('Ctrl Pts',(20.884926303708,-20.3402060495536,15.1061876671273));
#148640=CARTESIAN_POINT('Ctrl Pts',(20.8371054979832,-20.4143009787113,
15.1105741291398));
#148641=CARTESIAN_POINT('Ctrl Pts',(20.7855062921192,-20.4858374838363,
15.1149605911524));
#148642=CARTESIAN_POINT('Ctrl Pts',(20.7304530967375,-20.5544278556389,
15.1193470531649));
#148643=CARTESIAN_POINT('Ctrl Pts',(20.6753999013558,-20.6230182274415,
15.1237335151775));
#148644=CARTESIAN_POINT('Ctrl Pts',(20.6168931592929,-20.6886620833861,
15.12811997719));
#148645=CARTESIAN_POINT('Ctrl Pts',(20.5553006227462,-20.7510175211999,
15.1325064392025));
#148646=CARTESIAN_POINT('Ctrl Pts',(20.4965457256971,-20.810500171771,15.1366908118296));
#148647=CARTESIAN_POINT('Ctrl Pts',(20.4347644264919,-20.8672121309936,
15.1408751844566));
#148648=CARTESIAN_POINT('Ctrl Pts',(20.3702485909567,-20.9208297408847,
15.1450595570836));
#148649=CARTESIAN_POINT('Ctrl Pts',(20.3450868338478,-20.9417410918058,
15.146691500107));
#148650=CARTESIAN_POINT('Ctrl Pts',(20.3195095726725,-20.9621821194541,
15.1483234431303));
#148651=CARTESIAN_POINT('Ctrl Pts',(20.2935357468249,-20.9821350335323,
15.1499553861536));
#148652=CARTESIAN_POINT('Ctrl Pts',(20.2947698132858,-20.9837129250579,
14.3497865232697));
#148653=CARTESIAN_POINT('Ctrl Pts',(20.1912477797316,-21.0647995005029,
14.3563415485511));
#148654=CARTESIAN_POINT('Ctrl Pts',(19.3719149991153,-21.60811723892,14.405288509393));
#148655=CARTESIAN_POINT('Ctrl Pts',(17.2895133775451,-21.6122159629899,
14.4966274057954));
#148656=CARTESIAN_POINT('Ctrl Pts',(16.2008983314107,-19.9284205945985,
14.5845735760146));
#148657=CARTESIAN_POINT('Ctrl Pts',(16.1700292378907,-19.0164624118087,
14.6301278106733));
#148658=CARTESIAN_POINT('Ctrl Pts',(16.1703790167221,-18.9531317273334,
14.6332901097715));
#148659=CARTESIAN_POINT('',(16.1743645121285,-18.9514398261319,14.566709915053));
#148660=CARTESIAN_POINT('Ctrl Pts',(20.2923704978253,-20.9805871927218,
14.2834124327049));
#148661=CARTESIAN_POINT('Ctrl Pts',(19.8237022393519,-21.3341891611517,
14.3125636734706));
#148662=CARTESIAN_POINT('Ctrl Pts',(18.3750627815534,-21.8243382151095,
14.3841068497969));
#148663=CARTESIAN_POINT('Ctrl Pts',(16.5197423660721,-20.7321305462553,
14.478539335638));
#148664=CARTESIAN_POINT('Ctrl Pts',(16.1790023713152,-19.4133917175901,
14.5438205807135));
#148665=CARTESIAN_POINT('Ctrl Pts',(16.1781028623508,-18.9514411453429,
14.5667098902285));
#148666=CARTESIAN_POINT('Ctrl Pts',(16.1740000613162,-18.9514396975223,
14.5667099174731));
#148667=CARTESIAN_POINT('Ctrl Pts',(16.1740197372988,-18.8615409084374,
14.571157199272));
#148668=CARTESIAN_POINT('Ctrl Pts',(16.1787790795978,-18.7717655181971,
14.575604481071));
#148669=CARTESIAN_POINT('Ctrl Pts',(16.1882138900512,-18.6826060832318,
14.58005176287));
#148670=CARTESIAN_POINT('Ctrl Pts',(16.1976832329536,-18.5931203148802,
14.5845153222119));
#148671=CARTESIAN_POINT('Ctrl Pts',(16.211862232535,-18.504255369482,14.5889788815538));
#148672=CARTESIAN_POINT('Ctrl Pts',(16.23063522025,-18.4164957707849,14.5934424408956));
#148673=CARTESIAN_POINT('Ctrl Pts',(16.2494446598934,-18.3285657673207,
14.5979146672301));
#148674=CARTESIAN_POINT('Ctrl Pts',(16.2728657964755,-18.241745739755,14.6023868935646));
#148675=CARTESIAN_POINT('Ctrl Pts',(16.3007333122773,-18.1565044145825,
14.606859119899));
#148676=CARTESIAN_POINT('Ctrl Pts',(16.3286838403159,-18.0710091710796,
14.6113446681784));
#148677=CARTESIAN_POINT('Ctrl Pts',(16.3611071025136,-17.9871023685302,
14.6158302164579));
#148678=CARTESIAN_POINT('Ctrl Pts',(16.3977895032111,-17.9052333045547,
14.6203157647373));
#148679=CARTESIAN_POINT('Ctrl Pts',(16.4111522146039,-17.8754099382236,
14.6219497659465));
#148680=CARTESIAN_POINT('Ctrl Pts',(16.4250796827618,-17.8458567318514,
14.6235837671557));
#148681=CARTESIAN_POINT('Ctrl Pts',(16.4395601204677,-17.8165945045,14.625217768365));
#148682=CARTESIAN_POINT('Ctrl Pts',(16.4766441429939,-17.7416547050056,
14.629402402758));
#148683=CARTESIAN_POINT('Ctrl Pts',(16.5174725051856,-17.6683941847451,
14.6335870371511));
#148684=CARTESIAN_POINT('Ctrl Pts',(16.5618698248529,-17.5972120083883,
14.6377716715441));
#148685=CARTESIAN_POINT('Ctrl Pts',(16.6062039504309,-17.526131151049,14.6419503496281));
#148686=CARTESIAN_POINT('Ctrl Pts',(16.6540967016935,-17.4571231485616,
14.646129027712));
#148687=CARTESIAN_POINT('Ctrl Pts',(16.7053259809371,-17.3905642106128,
14.6503077057959));
#148688=CARTESIAN_POINT('Ctrl Pts',(16.7574735081934,-17.3228122515363,
14.6545612836814));
#148689=CARTESIAN_POINT('Ctrl Pts',(16.8130781406444,-17.2575984516733,
14.6588148615668));
#148690=CARTESIAN_POINT('Ctrl Pts',(16.8718583319471,-17.1952904599505,
14.6630684394522));
#148691=CARTESIAN_POINT('Ctrl Pts',(16.9294989545412,-17.1341904302313,
14.6672395534302));
#148692=CARTESIAN_POINT('Ctrl Pts',(16.9901927757376,-17.0758848946116,
14.6714106674081));
#148693=CARTESIAN_POINT('Ctrl Pts',(17.0536336491124,-17.0206872529793,
14.6755817813861));
#148694=CARTESIAN_POINT('Ctrl Pts',(17.1170532342894,-16.9655081334488,
14.6797514957065));
#148695=CARTESIAN_POINT('Ctrl Pts',(17.1832176941668,-16.9134351384329,
14.6839212100268));
#148696=CARTESIAN_POINT('Ctrl Pts',(17.2517856166926,-16.8647433023424,
14.6880909243472));
#148697=CARTESIAN_POINT('Ctrl Pts',(17.3203510992775,-16.8160531989163,
14.6922604902913));
#148698=CARTESIAN_POINT('Ctrl Pts',(17.3913194988899,-16.7707442808557,
14.6964300562353));
#148699=CARTESIAN_POINT('Ctrl Pts',(17.4643191824368,-16.7290491185112,
14.7005996221793));
#148700=CARTESIAN_POINT('Ctrl Pts',(17.5398854448024,-16.6858880056951,
14.7049157849183));
#148701=CARTESIAN_POINT('Ctrl Pts',(17.6176280306768,-16.6465997576134,
14.7092319476572));
#148702=CARTESIAN_POINT('Ctrl Pts',(17.6971072733112,-16.6113903628884,
14.7135481103961));
#148703=CARTESIAN_POINT('Ctrl Pts',(17.7739974879764,-16.5773279104931,
14.7177236745878));
#148704=CARTESIAN_POINT('Ctrl Pts',(17.8525124972025,-16.5470827802973,
14.7218992387795));
#148705=CARTESIAN_POINT('Ctrl Pts',(17.9322359204945,-16.5207915842498,
14.7260748029711));
#148706=CARTESIAN_POINT('Ctrl Pts',(18.0159859843727,-16.4931724823913,
14.7304612649837));
#148707=CARTESIAN_POINT('Ctrl Pts',(18.1010691812454,-16.4699173921691,
14.7348477269962));
#148708=CARTESIAN_POINT('Ctrl Pts',(18.1869895560292,-16.4511242385542,
14.7392341890088));
#148709=CARTESIAN_POINT('Ctrl Pts',(18.272909930813,-16.4323310849393,14.7436206510213));
#148710=CARTESIAN_POINT('Ctrl Pts',(18.3596668986516,-16.4179998874471,
14.7480071130339));
#148711=CARTESIAN_POINT('Ctrl Pts',(18.446759550604,-16.4081657042506,14.7523935750464));
#148712=CARTESIAN_POINT('Ctrl Pts',(18.5298449405377,-16.3987840064008,
14.7565782094394));
#148713=CARTESIAN_POINT('Ctrl Pts',(18.6135450624313,-16.3934596676543,
14.7607628438325));
#148714=CARTESIAN_POINT('Ctrl Pts',(18.6974294349979,-16.3922612254811,
14.7649474782255));
#148715=CARTESIAN_POINT('Ctrl Pts',(18.7811944085429,-16.3910644891421,
14.7691261563095));
#148716=CARTESIAN_POINT('Ctrl Pts',(18.8651426557822,-16.3939819908556,
14.7733048343934));
#148717=CARTESIAN_POINT('Ctrl Pts',(18.9488376266314,-16.4010306167687,
14.7774835124774));
#148718=CARTESIAN_POINT('Ctrl Pts',(19.0340327696825,-16.4082055842356,
14.7817370903628));
#148719=CARTESIAN_POINT('Ctrl Pts',(19.1189649879801,-16.4196612875147,
14.7859906682482));
#148720=CARTESIAN_POINT('Ctrl Pts',(19.2031727512631,-16.4353599920783,
14.7902442461337));
#148721=CARTESIAN_POINT('Ctrl Pts',(19.285747982737,-16.4507543466204,14.7944153601116));
#148722=CARTESIAN_POINT('Ctrl Pts',(19.3676261254063,-16.4702285646622,
14.7985864740896));
#148723=CARTESIAN_POINT('Ctrl Pts',(19.4483779483093,-16.493694862925,14.8027575880675));
#148724=CARTESIAN_POINT('Ctrl Pts',(19.5291026741582,-16.5171532868448,
14.8069273023879));
#148725=CARTESIAN_POINT('Ctrl Pts',(19.6087013894598,-16.5446010022893,
14.8110970167083));
#148726=CARTESIAN_POINT('Ctrl Pts',(19.6867580339315,-16.5758998066624,
14.8152667310286));
#148727=CARTESIAN_POINT('Ctrl Pts',(19.7648119008129,-16.6071974972898,
14.8194362969727));
#148728=CARTESIAN_POINT('Ctrl Pts',(19.8413233792982,-16.6423458323765,
14.8236058629167));
#148729=CARTESIAN_POINT('Ctrl Pts',(19.9158957565829,-16.6811582132233,
14.8277754288608));
#148730=CARTESIAN_POINT('Ctrl Pts',(19.993090006658,-16.7213351895004,14.8320915915997));
#148731=CARTESIAN_POINT('Ctrl Pts',(20.0682057930236,-16.7654384176637,
14.8364077543386));
#148732=CARTESIAN_POINT('Ctrl Pts',(20.1408319285747,-16.8132097052907,
14.8407239170775));
#148733=CARTESIAN_POINT('Ctrl Pts',(20.2110922753992,-16.8594248482479,
14.8448994812692));
#148734=CARTESIAN_POINT('Ctrl Pts',(20.2790223288375,-16.9090724304067,
14.8490750454609));
#148735=CARTESIAN_POINT('Ctrl Pts',(20.3442818409952,-16.9618762871215,
14.8532506096526));
#148736=CARTESIAN_POINT('Ctrl Pts',(20.4128374559721,-17.0173471411098,
14.8576370716651));
#148737=CARTESIAN_POINT('Ctrl Pts',(20.4784452273879,-17.0763011057023,
14.8620235336777));
#148738=CARTESIAN_POINT('Ctrl Pts',(20.5407543647586,-17.13837416609,14.8664099956902));
#148739=CARTESIAN_POINT('Ctrl Pts',(20.6030635021293,-17.2004472264776,
14.8707964577027));
#148740=CARTESIAN_POINT('Ctrl Pts',(20.6620736724741,-17.2656389014522,
14.8751829197153));
#148741=CARTESIAN_POINT('Ctrl Pts',(20.7174842649081,-17.3335469821889,
14.8795693817278));
#148742=CARTESIAN_POINT('Ctrl Pts',(20.770345333846,-17.398330511467,14.8837540161209));
#148743=CARTESIAN_POINT('Ctrl Pts',(20.8201275486196,-17.4658271045687,
14.8879386505139));
#148744=CARTESIAN_POINT('Ctrl Pts',(20.866540268707,-17.5357118928893,14.892123284907));
#148745=CARTESIAN_POINT('Ctrl Pts',(20.912886926032,-17.6054972088638,14.8963019629909));
#148746=CARTESIAN_POINT('Ctrl Pts',(20.9558733628218,-17.6776635880367,
14.9004806410749));
#148747=CARTESIAN_POINT('Ctrl Pts',(20.9952490842181,-17.7518531010236,
14.9046593191588));
#148748=CARTESIAN_POINT('Ctrl Pts',(21.0353305871216,-17.8273724077116,
14.9089128970442));
#148749=CARTESIAN_POINT('Ctrl Pts',(21.0716703524657,-17.9049877173954,
14.9131664749297));
#148750=CARTESIAN_POINT('Ctrl Pts',(21.1040502914402,-17.9842905311797,
14.9174200528151));
#148751=CARTESIAN_POINT('Ctrl Pts',(21.1358024821133,-18.0620559051722,
14.9215911667931));
#148752=CARTESIAN_POINT('Ctrl Pts',(21.1637468322872,-18.1414434905284,
14.925762280771));
#148753=CARTESIAN_POINT('Ctrl Pts',(21.1877248192283,-18.222044856513,14.929933394749));
#148754=CARTESIAN_POINT('Ctrl Pts',(21.2116947601243,-18.3026191759307,
14.9341031090694));
#148755=CARTESIAN_POINT('Ctrl Pts',(21.2317008500143,-18.3844060265126,
14.9382728233897));
#148756=CARTESIAN_POINT('Ctrl Pts',(21.2476340898709,-18.46698076096,14.9424425377101));
#148757=CARTESIAN_POINT('Ctrl Pts',(21.2635667627544,-18.5495525570439,
14.9466121036542));
#148758=CARTESIAN_POINT('Ctrl Pts',(21.2754267874402,-18.6329117293876,
14.9507816695982));
#148759=CARTESIAN_POINT('Ctrl Pts',(21.2831563307877,-18.7166237029669,
14.9549512355422));
#148760=CARTESIAN_POINT('Ctrl Pts',(21.2911576353439,-18.8032788862672,
14.9592673982812));
#148761=CARTESIAN_POINT('Ctrl Pts',(21.2947325504218,-18.8903116161907,
14.9635835610201));
#148762=CARTESIAN_POINT('Ctrl Pts',(21.2938756072079,-18.9772363947924,
14.967899723759));
#148763=CARTESIAN_POINT('Ctrl Pts',(21.293046578829,-19.0613296078741,14.9720752879507));
#148764=CARTESIAN_POINT('Ctrl Pts',(21.2880700686645,-19.1453213272334,
14.9762508521424));
#148765=CARTESIAN_POINT('Ctrl Pts',(21.2789941177451,-19.2287759755517,
14.9804264163341));
#148766=CARTESIAN_POINT('Ctrl Pts',(21.2694597621209,-19.3164457197619,
14.9848128783466));
#148767=CARTESIAN_POINT('Ctrl Pts',(21.2554010498833,-19.4035221357511,
14.9891993403591));
#148768=CARTESIAN_POINT('Ctrl Pts',(21.2369341836446,-19.4895132299242,
14.9935858023717));
#148769=CARTESIAN_POINT('Ctrl Pts',(21.2184673174058,-19.5755043240972,
14.9979722643842));
#148770=CARTESIAN_POINT('Ctrl Pts',(21.1955925215497,-19.6604095560011,
15.0023587263968));
#148771=CARTESIAN_POINT('Ctrl Pts',(21.1684852750765,-19.7437584514458,
15.0067451884093));
#148772=CARTESIAN_POINT('Ctrl Pts',(21.1426284959746,-19.8232624313143,
15.0109293012962));
#148773=CARTESIAN_POINT('Ctrl Pts',(21.112824919157,-19.9016463915127,15.0151134141831));
#148774=CARTESIAN_POINT('Ctrl Pts',(21.0791903430324,-19.9784902605226,
15.01929752707));
#148775=CARTESIAN_POINT('Ctrl Pts',(21.0456010518522,-20.0552306684295,
15.023476006548));
#148776=CARTESIAN_POINT('Ctrl Pts',(21.0081911857059,-20.1304346847173,
15.027654486026));
#148777=CARTESIAN_POINT('Ctrl Pts',(20.967126087575,-20.2036979975186,15.031832965504));
#148778=CARTESIAN_POINT('Ctrl Pts',(20.9250013387184,-20.2788518092133,
15.036119267172));
#148779=CARTESIAN_POINT('Ctrl Pts',(20.8790302479734,-20.3519629039354,
15.0404055688399));
#148780=CARTESIAN_POINT('Ctrl Pts',(20.8294436809226,-20.422617482584,15.0446918705079));
#148781=CARTESIAN_POINT('Ctrl Pts',(20.7811918137342,-20.4913702829484,
15.0488627996751));
#148782=CARTESIAN_POINT('Ctrl Pts',(20.7295169285826,-20.5577967390327,
15.0530337288422));
#148783=CARTESIAN_POINT('Ctrl Pts',(20.6746769388215,-20.6215427575017,
15.0572046580094));
#148784=CARTESIAN_POINT('Ctrl Pts',(20.6175615471624,-20.6879337037333,
15.0615486459278));
#148785=CARTESIAN_POINT('Ctrl Pts',(20.5570129676201,-20.751416498399,15.0658926338461));
#148786=CARTESIAN_POINT('Ctrl Pts',(20.4933694474881,-20.811628765976,15.0702366217645));
#148787=CARTESIAN_POINT('Ctrl Pts',(20.4297259273561,-20.871841033553,15.0745806096829));
#148788=CARTESIAN_POINT('Ctrl Pts',(20.3629878766118,-20.9287823858972,
15.0789245976012));
#148789=CARTESIAN_POINT('Ctrl Pts',(20.2935357468249,-20.9821350335323,
15.0832685855196));
#148790=CARTESIAN_POINT('Origin',(18.734,-18.952,-1.76670989022851));
#148791=CARTESIAN_POINT('',(20.2935357468249,-20.9821350335323,15.9499155251885));
#148792=CARTESIAN_POINT('',(20.2954006447972,-20.9845255200926,15.8832287071313));
#148793=CARTESIAN_POINT('',(20.2935357468249,-20.9821350335323,-1.76670989022851));
#148794=CARTESIAN_POINT('',(16.174000571626,-18.9537107672549,15.4332901097416));
#148795=CARTESIAN_POINT('Ctrl Pts',(16.1740005716256,-18.9537107666516,
15.4332901097715));
#148796=CARTESIAN_POINT('Ctrl Pts',(16.1739440307447,-18.8691027211111,
15.437482057942));
#148797=CARTESIAN_POINT('Ctrl Pts',(16.1780862675835,-18.7844696898645,
15.4416740061124));
#148798=CARTESIAN_POINT('Ctrl Pts',(16.1864081330308,-18.7002547332075,
15.4458659542829));
#148799=CARTESIAN_POINT('Ctrl Pts',(16.1947304086796,-18.6160356254258,
15.4500581090829));
#148800=CARTESIAN_POINT('Ctrl Pts',(16.2072326772703,-18.5322350838834,
15.4542502638829));
#148801=CARTESIAN_POINT('Ctrl Pts',(16.2238439368849,-18.4492908009531,
15.4584424186829));
#148802=CARTESIAN_POINT('Ctrl Pts',(16.2404607969944,-18.3663185533138,
15.4626359868701));
#148803=CARTESIAN_POINT('Ctrl Pts',(16.2611893110379,-18.2842035816671,
15.4668295550574));
#148804=CARTESIAN_POINT('Ctrl Pts',(16.2859076895265,-18.2033718951305,
15.4710231232446));
#148805=CARTESIAN_POINT('Ctrl Pts',(16.3106584247114,-18.122434398808,15.4752221808701));
#148806=CARTESIAN_POINT('Ctrl Pts',(16.3394093150966,-18.0427839738199,
15.4794212384956));
#148807=CARTESIAN_POINT('Ctrl Pts',(16.3719892689075,-17.9648296468169,
15.4836202961211));
#148808=CARTESIAN_POINT('Ctrl Pts',(16.4045936038559,-17.8868169828627,
15.4878224961022));
#148809=CARTESIAN_POINT('Ctrl Pts',(16.4410325111314,-17.8105033515335,
15.4920246960833));
#148810=CARTESIAN_POINT('Ctrl Pts',(16.4810885578785,-17.7362738655611,
15.4962268960645));
#148811=CARTESIAN_POINT('Ctrl Pts',(16.5212156880346,-17.6619126520384,
15.5004365532643));
#148812=CARTESIAN_POINT('Ctrl Pts',(16.5649725361192,-17.5896433529152,
15.5046462104641));
#148813=CARTESIAN_POINT('Ctrl Pts',(16.612098119287,-17.5198224940229,15.5088558676639));
#148814=CARTESIAN_POINT('Ctrl Pts',(16.6314200308983,-17.4911953158863,
15.5105818648582));
#148815=CARTESIAN_POINT('Ctrl Pts',(16.6513077816386,-17.4629793510679,
15.5123078620525));
#148816=CARTESIAN_POINT('Ctrl Pts',(16.6717415022699,-17.4351974787271,
15.5140338592469));
#148817=CARTESIAN_POINT('Ctrl Pts',(16.7212825156696,-17.3678410665133,
15.5182184936399));
#148818=CARTESIAN_POINT('Ctrl Pts',(16.7742191330187,-17.3027889832897,
15.522403128033));
#148819=CARTESIAN_POINT('Ctrl Pts',(16.8303093008605,-17.2404037502934,
15.526587762426));
#148820=CARTESIAN_POINT('Ctrl Pts',(16.8863196312909,-17.1781073149545,
15.53076644051));
#148821=CARTESIAN_POINT('Ctrl Pts',(16.9454742913219,-17.1184705290969,
15.5349451185939));
#148822=CARTESIAN_POINT('Ctrl Pts',(17.0074891937055,-17.0618252896231,
15.5391237966778));
#148823=CARTESIAN_POINT('Ctrl Pts',(17.070615668645,-17.004164724942,15.5433773745633));
#148824=CARTESIAN_POINT('Ctrl Pts',(17.1367056485332,-16.949604396855,15.5476309524487));
#148825=CARTESIAN_POINT('Ctrl Pts',(17.2054179892121,-16.8984574422974,
15.5518845303342));
#148826=CARTESIAN_POINT('Ctrl Pts',(17.272798207086,-16.8483020712589,15.5560556443121));
#148827=CARTESIAN_POINT('Ctrl Pts',(17.3426996279386,-16.8014291923403,
15.5602267582901));
#148828=CARTESIAN_POINT('Ctrl Pts',(17.4147663076937,-16.7580942442566,
15.564397872268));
#148829=CARTESIAN_POINT('Ctrl Pts',(17.4868088047783,-16.7147738376334,
15.5685675865884));
#148830=CARTESIAN_POINT('Ctrl Pts',(17.5610147238612,-16.6749892409427,
15.5727373009088));
#148831=CARTESIAN_POINT('Ctrl Pts',(17.6370000578043,-16.6389519834594,
15.5769070152291));
#148832=CARTESIAN_POINT('Ctrl Pts',(17.7129826878632,-16.6029160083363,
15.5810765811732));
#148833=CARTESIAN_POINT('Ctrl Pts',(17.7907441908667,-16.5706273036551,
15.5852461471172));
#148834=CARTESIAN_POINT('Ctrl Pts',(17.8698781766136,-16.5422503295265,
15.5894157130613));
#148835=CARTESIAN_POINT('Ctrl Pts',(17.951794415677,-16.5128756559943,15.5937318758002));
#148836=CARTESIAN_POINT('Ctrl Pts',(18.0351809497172,-16.4876930819298,
15.5980480385391));
#148837=CARTESIAN_POINT('Ctrl Pts',(18.1195690084031,-16.4668290689441,
15.602364201278));
#148838=CARTESIAN_POINT('Ctrl Pts',(18.2012081349533,-16.4466446989869,
15.6065397654697));
#148839=CARTESIAN_POINT('Ctrl Pts',(18.2837840674898,-16.4305019005907,
15.6107153296614));
#148840=CARTESIAN_POINT('Ctrl Pts',(18.3668630221883,-16.4184628600466,
15.6148908938531));
#148841=CARTESIAN_POINT('Ctrl Pts',(18.4541380973871,-16.4058157561848,
15.6192773558656));
#148842=CARTESIAN_POINT('Ctrl Pts',(18.5419677640929,-16.3976979204099,
15.6236638178781));
#148843=CARTESIAN_POINT('Ctrl Pts',(18.6298465962985,-16.3941196141146,
15.6280502798907));
#148844=CARTESIAN_POINT('Ctrl Pts',(18.7177254285042,-16.3905413078192,
15.6324367419032));
#148845=CARTESIAN_POINT('Ctrl Pts',(18.8056528468588,-16.391502448601,15.6368232039158));
#148846=CARTESIAN_POINT('Ctrl Pts',(18.8931294701919,-16.3969505265619,
15.6412096659283));
#148847=CARTESIAN_POINT('Ctrl Pts',(18.9765811644139,-16.4021479303798,
15.6453943003213));
#148848=CARTESIAN_POINT('Ctrl Pts',(19.0599332586381,-16.4114477893304,
15.6495789347144));
#148849=CARTESIAN_POINT('Ctrl Pts',(19.1427499109294,-16.4248428006325,
15.6537635691074));
#148850=CARTESIAN_POINT('Ctrl Pts',(19.2254486839666,-16.4382187457938,
15.6579422471914));
#148851=CARTESIAN_POINT('Ctrl Pts',(19.3076130786645,-16.4556781923683,
15.6621209252753));
#148852=CARTESIAN_POINT('Ctrl Pts',(19.3888102512128,-16.4771619174365,
15.6662996033592));
#148853=CARTESIAN_POINT('Ctrl Pts',(19.4714628247241,-16.4990307228366,
15.6705531812447));
#148854=CARTESIAN_POINT('Ctrl Pts',(19.5531126789041,-16.5250694661815,
15.6748067591301));
#148855=CARTESIAN_POINT('Ctrl Pts',(19.633311860283,-16.5551607943055,15.6790603370155));
#148856=CARTESIAN_POINT('Ctrl Pts',(19.7119562240349,-16.5846687433154,
15.6832314509935));
#148857=CARTESIAN_POINT('Ctrl Pts',(19.7892052107338,-16.6180733757685,
15.6874025649714));
#148858=CARTESIAN_POINT('Ctrl Pts',(19.8646513710665,-16.6552136631577,
15.6915736789494));
#148859=CARTESIAN_POINT('Ctrl Pts',(19.9400722147116,-16.6923414877648,
15.6957433932698));
#148860=CARTESIAN_POINT('Ctrl Pts',(20.0136910210525,-16.733202274758,15.6999131075901));
#148861=CARTESIAN_POINT('Ctrl Pts',(20.085122071664,-16.7775876316893,15.7040828219105));
#148862=CARTESIAN_POINT('Ctrl Pts',(20.1565505804521,-16.8219714091991,
15.7082523878546));
#148863=CARTESIAN_POINT('Ctrl Pts',(20.2257910980031,-16.8698792637602,
15.7124219537986));
#148864=CARTESIAN_POINT('Ctrl Pts',(20.2924853680819,-16.9210585046647,
15.7165915197426));
#148865=CARTESIAN_POINT('Ctrl Pts',(20.3615245264204,-16.974037144543,15.7209076824816));
#148866=CARTESIAN_POINT('Ctrl Pts',(20.4278346353052,-17.03052117375,15.7252238452205));
#148867=CARTESIAN_POINT('Ctrl Pts',(20.4910556240452,-17.0901848818932,
15.7295400079594));
#148868=CARTESIAN_POINT('Ctrl Pts',(20.5522171957265,-17.147905051019,15.7337155721511));
#148869=CARTESIAN_POINT('Ctrl Pts',(20.61048752063,-17.2086005517579,15.7378911363428));
#148870=CARTESIAN_POINT('Ctrl Pts',(20.6655795109694,-17.2719403008216,
15.7420667005344));
#148871=CARTESIAN_POINT('Ctrl Pts',(20.7234540667722,-17.3384791900349,
15.746453162547));
#148872=CARTESIAN_POINT('Ctrl Pts',(20.7778204147501,-17.4079360098505,
15.7508396245595));
#148873=CARTESIAN_POINT('Ctrl Pts',(20.8283963491844,-17.4798913312792,
15.7552260865721));
#148874=CARTESIAN_POINT('Ctrl Pts',(20.8789722836188,-17.5518466527079,
15.7596125485847));
#148875=CARTESIAN_POINT('Ctrl Pts',(20.9257575602052,-17.6262999440045,
15.7639990105972));
#148876=CARTESIAN_POINT('Ctrl Pts',(20.9685260259021,-17.7028028820213,
15.7683854726098));
#148877=CARTESIAN_POINT('Ctrl Pts',(21.009326651094,-17.7757858064551,15.7725701070028));
#148878=CARTESIAN_POINT('Ctrl Pts',(21.0466238491571,-17.850905564207,15.7767547413958));
#148879=CARTESIAN_POINT('Ctrl Pts',(21.0801878476018,-17.9277917283259,
15.7809393757889));
#148880=CARTESIAN_POINT('Ctrl Pts',(21.1137040718491,-18.0045684545068,
15.7851180538728));
#148881=CARTESIAN_POINT('Ctrl Pts',(21.1434974687763,-18.0831061749367,
15.7892967319568));
#148882=CARTESIAN_POINT('Ctrl Pts',(21.1693835453415,-18.1630088802274,
15.7934754100407));
#148883=CARTESIAN_POINT('Ctrl Pts',(21.195733611225,-18.2443437840853,15.7977289879262));
#148884=CARTESIAN_POINT('Ctrl Pts',(21.218034666248,-18.3270926679897,15.8019825658116));
#148885=CARTESIAN_POINT('Ctrl Pts',(21.2361429171342,-18.41081535292,15.806236143697));
#148886=CARTESIAN_POINT('Ctrl Pts',(21.2539001042416,-18.4929149102316,
15.810407257675));
#148887=CARTESIAN_POINT('Ctrl Pts',(21.2676255061034,-18.575950377106,15.8145783716529));
#148888=CARTESIAN_POINT('Ctrl Pts',(21.2772339776254,-18.6594919914747,
15.8187494856309));
#148889=CARTESIAN_POINT('Ctrl Pts',(21.2868392249321,-18.7430055726479,
15.8229191999513));
#148890=CARTESIAN_POINT('Ctrl Pts',(21.2923302330118,-18.8270245073654,
15.8270889142716));
#148891=CARTESIAN_POINT('Ctrl Pts',(21.2936734448665,-18.9111116685929,
15.831258628592));
#148892=CARTESIAN_POINT('Ctrl Pts',(21.295016608924,-18.9951958376384,15.8354281945361));
#148893=CARTESIAN_POINT('Ctrl Pts',(21.2922122637205,-19.0793477683789,
15.8395977604801));
#148894=CARTESIAN_POINT('Ctrl Pts',(21.285278964847,-19.1631294473286,15.8437673264242));
#148895=CARTESIAN_POINT('Ctrl Pts',(21.2781018997383,-19.2498567867541,
15.8480834891631));
#148896=CARTESIAN_POINT('Ctrl Pts',(21.2665001742353,-19.3361868282292,
15.852399651902));
#148897=CARTESIAN_POINT('Ctrl Pts',(21.2505527597975,-19.4216405084271,
15.8567158146409));
#148898=CARTESIAN_POINT('Ctrl Pts',(21.2351248307076,-19.5043105439807,
15.8608913788326));
#148899=CARTESIAN_POINT('Ctrl Pts',(21.2156301415435,-19.5861599891146,
15.8650669430243));
#148900=CARTESIAN_POINT('Ctrl Pts',(21.1921916857819,-19.6667682393284,
15.8692425072159));
#148901=CARTESIAN_POINT('Ctrl Pts',(21.1675694093395,-19.7514478206324,
15.8736289692285));
#148902=CARTESIAN_POINT('Ctrl Pts',(21.1385946886758,-19.8347569748338,
15.878015431241));
#148903=CARTESIAN_POINT('Ctrl Pts',(21.1054674445918,-19.9162313826263,
15.8824018932535));
#148904=CARTESIAN_POINT('Ctrl Pts',(21.0723402005077,-19.9977057904188,
15.8867883552661));
#148905=CARTESIAN_POINT('Ctrl Pts',(21.0350607478796,-20.0773449585575,
15.8911748172786));
#148906=CARTESIAN_POINT('Ctrl Pts',(20.9938836431737,-20.1547160593073,
15.8955612792911));
#148907=CARTESIAN_POINT('Ctrl Pts',(20.9545971350275,-20.2285347602967,
15.8997463422483));
#148908=CARTESIAN_POINT('Ctrl Pts',(20.9116167922609,-20.3005638940076,
15.9039314052055));
#148909=CARTESIAN_POINT('Ctrl Pts',(20.8651297737826,-20.3704096331094,
15.9081164681627));
#148910=CARTESIAN_POINT('Ctrl Pts',(20.8187208419206,-20.4401380487601,
15.9122945012561));
#148911=CARTESIAN_POINT('Ctrl Pts',(20.7688171985821,-20.5076899820961,
15.9164725343495));
#148912=CARTESIAN_POINT('Ctrl Pts',(20.7156518556524,-20.5726961229637,
15.920650567443));
#148913=CARTESIAN_POINT('Ctrl Pts',(20.6625380463667,-20.6376392527956,
15.9248245507314));
#148914=CARTESIAN_POINT('Ctrl Pts',(20.6061691036063,-20.7000411350043,
15.9289985340199));
#148915=CARTESIAN_POINT('Ctrl Pts',(20.546820818089,-20.7595620823372,15.9331725173083));
#148916=CARTESIAN_POINT('Ctrl Pts',(20.4875162743664,-20.8190391606174,
15.9373434242228));
#148917=CARTESIAN_POINT('Ctrl Pts',(20.4252370755883,-20.8756391988914,
15.9415143311373));
#148918=CARTESIAN_POINT('Ctrl Pts',(20.3602977399997,-20.9290573236181,
15.9456852380518));
#148919=CARTESIAN_POINT('Ctrl Pts',(20.3383431194471,-20.9471168656256,
15.947095333764));
#148920=CARTESIAN_POINT('Ctrl Pts',(20.3160847638627,-20.9648130339878,
15.9485054294762));
#148921=CARTESIAN_POINT('Ctrl Pts',(20.2935357468249,-20.9821350335323,
15.9499155251885));
#148922=CARTESIAN_POINT('Ctrl Pts',(20.2935357468249,-20.9821350335323,
15.1499553861536));
#148923=CARTESIAN_POINT('Ctrl Pts',(20.2270593471735,-21.0332017457777,
15.1541321176549));
#148924=CARTESIAN_POINT('Ctrl Pts',(20.157982906757,-21.081068370004,15.1583088491561));
#148925=CARTESIAN_POINT('Ctrl Pts',(20.086648755646,-21.1254629842372,15.1624855806574));
#148926=CARTESIAN_POINT('Ctrl Pts',(20.015384561649,-21.1698140608515,15.166658216055));
#148927=CARTESIAN_POINT('Ctrl Pts',(19.9418674462888,-21.2106996525442,
15.1708308514525));
#148928=CARTESIAN_POINT('Ctrl Pts',(19.8664701158255,-21.2478901186168,
15.1750034868501));
#148929=CARTESIAN_POINT('Ctrl Pts',(19.7911123063922,-21.2850610905572,
15.1791739350767));
#148930=CARTESIAN_POINT('Ctrl Pts',(19.7138766504389,-21.318540579423,15.1833443833033));
#148931=CARTESIAN_POINT('Ctrl Pts',(19.6351609242639,-21.3481446092796,
15.1875148315299));
#148932=CARTESIAN_POINT('Ctrl Pts',(19.5564628454869,-21.3777420021639,
15.1916843447775));
#148933=CARTESIAN_POINT('Ctrl Pts',(19.4762857860939,-21.403465500195,15.195853858025));
#148934=CARTESIAN_POINT('Ctrl Pts',(19.3950467213204,-21.4251795794547,
15.2000233712725));
#148935=CARTESIAN_POINT('Ctrl Pts',(19.3138015000959,-21.4468953042486,
15.2041932004937));
#148936=CARTESIAN_POINT('Ctrl Pts',(19.2314945584613,-21.464600889432,15.2083630297148));
#148937=CARTESIAN_POINT('Ctrl Pts',(19.1485558905415,-21.4782112765201,
15.212532858936));
#148938=CARTESIAN_POINT('Ctrl Pts',(19.0655304261605,-21.4918359070663,
15.216707051941));
#148939=CARTESIAN_POINT('Ctrl Pts',(18.9818723702625,-21.5013567070332,
15.220881244946));
#148940=CARTESIAN_POINT('Ctrl Pts',(18.8980192295312,-21.5067402397003,
15.2250554379511));
#148941=CARTESIAN_POINT('Ctrl Pts',(18.8141207480157,-21.5121266833329,
15.2292318880115));
#148942=CARTESIAN_POINT('Ctrl Pts',(18.7300274318276,-21.513371398164,15.2334083380719));
#148943=CARTESIAN_POINT('Ctrl Pts',(18.6461767539422,-21.5104931263249,
15.2375847881324));
#148944=CARTESIAN_POINT('Ctrl Pts',(18.5621802082572,-21.5076098474043,
15.2417685036031));
#148945=CARTESIAN_POINT('Ctrl Pts',(18.4784276028385,-21.5005892941992,
15.2459522190739));
#148946=CARTESIAN_POINT('Ctrl Pts',(18.3953510434448,-21.4895020954128,
15.2501359345446));
#148947=CARTESIAN_POINT('Ctrl Pts',(18.3321636121995,-21.4810692520676,
15.2533180383244));
#148948=CARTESIAN_POINT('Ctrl Pts',(18.2693671652201,-21.4702849264138,
15.2565001421042));
#148949=CARTESIAN_POINT('Ctrl Pts',(18.20714644876,-21.4571996598167,15.259682245884));
#148950=CARTESIAN_POINT('Ctrl Pts',(18.125322923169,-21.4399918437196,15.263866880277));
#148951=CARTESIAN_POINT('Ctrl Pts',(18.0441910630359,-21.41873907309,15.2680515146701));
#148952=CARTESIAN_POINT('Ctrl Pts',(17.9641810754837,-21.3935115857715,
15.2722361490631));
#148953=CARTESIAN_POINT('Ctrl Pts',(17.8842849722453,-21.3683200066586,
15.2764148271471));
#148954=CARTESIAN_POINT('Ctrl Pts',(17.8055080047354,-21.3391650856198,
15.280593505231));
#148955=CARTESIAN_POINT('Ctrl Pts',(17.728269907104,-21.3061680017032,15.284772183315));
#148956=CARTESIAN_POINT('Ctrl Pts',(17.6496473720827,-21.2725794687721,
15.2890257612004));
#148957=CARTESIAN_POINT('Ctrl Pts',(17.5726198898779,-21.2350097758299,
15.2932793390859));
#148958=CARTESIAN_POINT('Ctrl Pts',(17.4976137413827,-21.1936398059239,
15.2975329169713));
#148959=CARTESIAN_POINT('Ctrl Pts',(17.4240617334387,-21.1530718736114,
15.3017040309492));
#148960=CARTESIAN_POINT('Ctrl Pts',(17.3524538049873,-21.1088499333756,
15.3058751449272));
#148961=CARTESIAN_POINT('Ctrl Pts',(17.2831698439507,-21.0611922288634,
15.3100462589051));
#148962=CARTESIAN_POINT('Ctrl Pts',(17.2139091318162,-21.0135505163542,
15.3142159732255));
#148963=CARTESIAN_POINT('Ctrl Pts',(17.1469712170494,-20.9624755897518,
15.3183856875459));
#148964=CARTESIAN_POINT('Ctrl Pts',(17.0827076373574,-20.9082294172919,
15.3225554018663));
#148965=CARTESIAN_POINT('Ctrl Pts',(17.0184463444393,-20.8539851751436,
15.3267249678103));
#148966=CARTESIAN_POINT('Ctrl Pts',(16.9568595483704,-20.7965702088949,
15.3308945337544));
#148967=CARTESIAN_POINT('Ctrl Pts',(16.8982652087742,-20.7362863492957,
15.3350640996984));
#148968=CARTESIAN_POINT('Ctrl Pts',(16.8376107644816,-20.6738829835612,
15.3393802624373));
#148969=CARTESIAN_POINT('Ctrl Pts',(16.7801634890496,-20.6084056085283,
15.3436964251763));
#148970=CARTESIAN_POINT('Ctrl Pts',(16.7262325806843,-20.5402285698017,
15.3480125879152));
#148971=CARTESIAN_POINT('Ctrl Pts',(16.6740584659864,-20.4742723909407,
15.3521881521069));
#148972=CARTESIAN_POINT('Ctrl Pts',(16.6251753803869,-20.4057901412944,
15.3563637162985));
#148973=CARTESIAN_POINT('Ctrl Pts',(16.5798195291698,-20.335150931422,15.3605392804902));
#148974=CARTESIAN_POINT('Ctrl Pts',(16.532172861731,-20.2609439029878,15.3649257425028));
#148975=CARTESIAN_POINT('Ctrl Pts',(16.488419403819,-20.1843567987727,15.3693122045153));
#148976=CARTESIAN_POINT('Ctrl Pts',(16.4487777573746,-20.1058454410405,
15.3736986665278));
#148977=CARTESIAN_POINT('Ctrl Pts',(16.4091361109301,-20.0273340833083,
15.3780851285404));
#148978=CARTESIAN_POINT('Ctrl Pts',(16.3736064408137,-19.9468990335382,
15.3824715905529));
#148979=CARTESIAN_POINT('Ctrl Pts',(16.3423477078172,-19.8650166007783,
15.3868580525655));
#148980=CARTESIAN_POINT('Ctrl Pts',(16.3083133302778,-19.7758633510063,
15.3916340140292));
#148981=CARTESIAN_POINT('Ctrl Pts',(16.2792349760223,-19.6847190703936,
15.396409975493));
#148982=CARTESIAN_POINT('Ctrl Pts',(16.2553188691393,-19.5921092496716,
15.4011859369567));
#148983=CARTESIAN_POINT('Ctrl Pts',(16.2315006236314,-19.4998783754247,
15.405942355852));
#148984=CARTESIAN_POINT('Ctrl Pts',(16.212802591162,-19.406194112186,15.4106987747473));
#148985=CARTESIAN_POINT('Ctrl Pts',(16.1993817363336,-19.3115973546745,
15.4154551936426));
#148986=CARTESIAN_POINT('Ctrl Pts',(16.1860549755609,-19.2176638181479,
15.4201782651282));
#148987=CARTESIAN_POINT('Ctrl Pts',(16.1779317634136,-19.1228307363238,
15.4249013366138));
#148988=CARTESIAN_POINT('Ctrl Pts',(16.1751178968034,-19.0276464271479,
15.4296244080995));
#148989=CARTESIAN_POINT('Ctrl Pts',(16.1743899245164,-19.0030214008619,
15.4308463086469));
#148990=CARTESIAN_POINT('Ctrl Pts',(16.1740170525925,-18.9783729560401,
15.4320682091942));
#148991=CARTESIAN_POINT('Ctrl Pts',(16.174000571626,-18.9537107672549,15.4332901097416));
#148992=CARTESIAN_POINT('',(16.1740008768645,-18.949881145288,15.3667098902285));
#148993=CARTESIAN_POINT('Ctrl Pts',(20.2935357468249,-20.9821350335323,
15.0832685855196));
#148994=CARTESIAN_POINT('Ctrl Pts',(20.2260494149554,-21.03397756875,15.0874896196505));
#148995=CARTESIAN_POINT('Ctrl Pts',(20.156001045364,-21.0824316029258,15.0917106537815));
#148996=CARTESIAN_POINT('Ctrl Pts',(20.0837719873172,-21.1272506941164,
15.0959316879124));
#148997=CARTESIAN_POINT('Ctrl Pts',(20.0123180971675,-21.1715887833167,
15.1001074215751));
#148998=CARTESIAN_POINT('Ctrl Pts',(19.9387305383576,-21.2123694058899,
15.1042831552377));
#148999=CARTESIAN_POINT('Ctrl Pts',(19.8634030839696,-21.2494004165404,
15.1084588889004));
#149000=CARTESIAN_POINT('Ctrl Pts',(19.7868498441635,-21.2870340238569,
15.1127025732655));
#149001=CARTESIAN_POINT('Ctrl Pts',(19.7085000337302,-21.3207947028272,
15.1169462576305));
#149002=CARTESIAN_POINT('Ctrl Pts',(19.6287860118066,-21.350532466546,15.1211899419956));
#149003=CARTESIAN_POINT('Ctrl Pts',(19.549071989883,-21.3802702302648,15.1254336263606));
#149004=CARTESIAN_POINT('Ctrl Pts',(19.4679942448969,-21.4059849931164,
15.1296773107257));
#149005=CARTESIAN_POINT('Ctrl Pts',(19.3859971465586,-21.4275806835729,
15.1339209950908));
#149006=CARTESIAN_POINT('Ctrl Pts',(19.3051410205324,-21.4488758745561,
15.1381056294838));
#149007=CARTESIAN_POINT('Ctrl Pts',(19.2230900288836,-21.4662452083819,
15.1422902638769));
#149008=CARTESIAN_POINT('Ctrl Pts',(19.1402602214101,-21.4795586308728,
15.1464748982699));
#149009=CARTESIAN_POINT('Ctrl Pts',(19.0575483119153,-21.4928531033548,
15.1506535763538));
#149010=CARTESIAN_POINT('Ctrl Pts',(18.974060238839,-21.5021030592902,15.1548322544378));
#149011=CARTESIAN_POINT('Ctrl Pts',(18.8902255244996,-21.5072286757734,
15.1590109325217));
#149012=CARTESIAN_POINT('Ctrl Pts',(18.8048881331567,-21.5124461652484,
15.1632645104072));
#149013=CARTESIAN_POINT('Ctrl Pts',(18.7191920174691,-21.5133898805874,
15.1675180882926));
#149014=CARTESIAN_POINT('Ctrl Pts',(18.6335993142633,-21.510030434202,15.171771666178));
#149015=CARTESIAN_POINT('Ctrl Pts',(18.5496659926296,-21.5067361172402,
15.175942780156));
#149016=CARTESIAN_POINT('Ctrl Pts',(18.4658325904026,-21.4993040188572,
15.1801138941339));
#149017=CARTESIAN_POINT('Ctrl Pts',(18.3825365202413,-21.4877589440631,
15.1842850081119));
#149018=CARTESIAN_POINT('Ctrl Pts',(18.2992684008808,-21.4762177433303,
15.1884547224323));
#149019=CARTESIAN_POINT('Ctrl Pts',(18.2165377107911,-21.4605663702896,
15.1926244367526));
#149020=CARTESIAN_POINT('Ctrl Pts',(18.1347761196902,-21.4408814237055,
15.196794151073));
#149021=CARTESIAN_POINT('Ctrl Pts',(18.0530174380175,-21.4211971775963,
15.200963717017));
#149022=CARTESIAN_POINT('Ctrl Pts',(17.9722282338226,-21.3974797518311,
15.2051332829611));
#149023=CARTESIAN_POINT('Ctrl Pts',(17.8928280294726,-21.3698564299807,
15.2093028489051));
#149024=CARTESIAN_POINT('Ctrl Pts',(17.8106362118883,-21.3412619062111,
15.213619011644));
#149025=CARTESIAN_POINT('Ctrl Pts',(17.729933384083,-21.3084818866878,15.217935174383));
#149026=CARTESIAN_POINT('Ctrl Pts',(17.6511637413075,-21.2717124039115,
15.2222513371219));
#149027=CARTESIAN_POINT('Ctrl Pts',(17.5749600113602,-21.2361406831691,
15.2264269013136));
#149028=CARTESIAN_POINT('Ctrl Pts',(17.5005658480113,-21.1968356830554,
15.2306024655052));
#149029=CARTESIAN_POINT('Ctrl Pts',(17.4283578509295,-21.1540214755017,
15.2347780296969));
#149030=CARTESIAN_POINT('Ctrl Pts',(17.3525027995735,-21.1090448241056,
15.2391644917095));
#149031=CARTESIAN_POINT('Ctrl Pts',(17.2790610511148,-21.0601954720667,
15.243550953722));
#149032=CARTESIAN_POINT('Ctrl Pts',(17.2084323379748,-21.007782894321,15.2479374157345));
#149033=CARTESIAN_POINT('Ctrl Pts',(17.1378036248349,-20.9553703165754,
15.252323877747));
#149034=CARTESIAN_POINT('Ctrl Pts',(17.0699883460669,-20.8993949411349,
15.2567103397596));
#149035=CARTESIAN_POINT('Ctrl Pts',(17.0053421035814,-20.8402112903883,
15.2610968017721));
#149036=CARTESIAN_POINT('Ctrl Pts',(16.9445899812057,-20.7845927075508,
15.2652190348167));
#149037=CARTESIAN_POINT('Ctrl Pts',(16.8863955977248,-20.7259204795934,
15.2693412678613));
#149038=CARTESIAN_POINT('Ctrl Pts',(16.8310887538618,-20.6644627847987,
15.2734635009059));
#149039=CARTESIAN_POINT('Ctrl Pts',(16.7758743514522,-20.6031078121671,
15.2775788439313));
#149040=CARTESIAN_POINT('Ctrl Pts',(16.7235382140149,-20.5389769727691,
15.2816941869567));
#149041=CARTESIAN_POINT('Ctrl Pts',(16.6743754759298,-20.4723771965696,
15.2858095299821));
#149042=CARTESIAN_POINT('Ctrl Pts',(16.6252589923643,-20.4058400804408,
15.2899210011073));
#149043=CARTESIAN_POINT('Ctrl Pts',(16.5793102664141,-20.336839014796,15.2940324722326));
#149044=CARTESIAN_POINT('Ctrl Pts',(16.5367853878613,-20.2657153223604,
15.2981439433578));
#149045=CARTESIAN_POINT('Ctrl Pts',(16.4942868717937,-20.1946357216976,
15.3022528656552));
#149046=CARTESIAN_POINT('Ctrl Pts',(16.4552082342186,-20.1214365120742,
15.3063617879525));
#149047=CARTESIAN_POINT('Ctrl Pts',(16.4197623875945,-20.0464881330228,
15.3104707102498));
#149048=CARTESIAN_POINT('Ctrl Pts',(16.3843271437787,-19.971562173052,15.3145784034577));
#149049=CARTESIAN_POINT('Ctrl Pts',(16.3525227351499,-19.894888512104,15.3186860966657));
#149050=CARTESIAN_POINT('Ctrl Pts',(16.3245154961056,-19.8168609284116,
15.3227937898736));
#149051=CARTESIAN_POINT('Ctrl Pts',(16.2964946934766,-19.7387955568548,
15.3269034723902));
#149052=CARTESIAN_POINT('Ctrl Pts',(16.272274898332,-19.6593753990486,15.3310131549069));
#149053=CARTESIAN_POINT('Ctrl Pts',(16.2519734104534,-19.5790119686126,
15.3351228374235));
#149054=CARTESIAN_POINT('Ctrl Pts',(16.231666738396,-19.4986280166076,15.3392335693868));
#149055=CARTESIAN_POINT('Ctrl Pts',(16.2152804642378,-19.4173007774467,
15.3433443013501));
#149056=CARTESIAN_POINT('Ctrl Pts',(16.2028808242122,-19.3354523672626,
15.3474550333134));
#149057=CARTESIAN_POINT('Ctrl Pts',(16.1904661338132,-19.2535046115225,
15.3515707547805));
#149058=CARTESIAN_POINT('Ctrl Pts',(16.1820477886731,-19.1710348943536,
15.3556864762476));
#149059=CARTESIAN_POINT('Ctrl Pts',(16.1776401048971,-19.0884700945614,
15.3598021977147));
#149060=CARTESIAN_POINT('Ctrl Pts',(16.1751742007241,-19.04227873994,15.362104761886));
#149061=CARTESIAN_POINT('Ctrl Pts',(16.173962657598,-18.9960576424388,15.3644073260572));
#149062=CARTESIAN_POINT('Ctrl Pts',(16.1740008768645,-18.949881145288,15.3667098902285));
#149063=CARTESIAN_POINT('Ctrl Pts',(16.1723624843679,-18.9498797892267,
15.3667098902285));
#149064=CARTESIAN_POINT('Ctrl Pts',(16.1710770695818,-18.8056440598866,
15.3738974629702));
#149065=CARTESIAN_POINT('Ctrl Pts',(16.2478506876061,-17.8120819459935,
15.4234769712724));
#149066=CARTESIAN_POINT('Ctrl Pts',(17.5479306946412,-16.1669449835732,
15.515448415135));
#149067=CARTESIAN_POINT('Ctrl Pts',(20.4337937048959,-16.4472059560846,
15.6426242218164));
#149068=CARTESIAN_POINT('Ctrl Pts',(21.7124086028558,-18.932560808362,15.7652176524819));
#149069=CARTESIAN_POINT('Ctrl Pts',(20.8926534809929,-20.5182931343282,
15.8454191475868));
#149070=CARTESIAN_POINT('Ctrl Pts',(20.2954006447972,-20.9845255200926,
15.8832287071313));
#149071=CARTESIAN_POINT('Origin',(18.734,-18.952,-1.76670989022851));
#149072=CARTESIAN_POINT('',(20.2935357468249,-20.9821350335323,16.7498176655673));
#149073=CARTESIAN_POINT('',(20.2935357468249,-20.9821350335323,16.6833822574076));
#149074=CARTESIAN_POINT('',(20.2935357468249,-20.9821350335323,-1.76670989022851));
#149075=CARTESIAN_POINT('',(16.1740007055014,-18.9500994299064,16.2332901098004));
#149076=CARTESIAN_POINT('Ctrl Pts',(16.1740007055014,-18.9500994299065,
16.2332901098004));
#149077=CARTESIAN_POINT('Ctrl Pts',(16.1740727513108,-18.8530563258851,
16.2381006886061));
#149078=CARTESIAN_POINT('Ctrl Pts',(16.1796667621363,-18.7562381388328,
16.2429112674118));
#149079=CARTESIAN_POINT('Ctrl Pts',(16.1906824963738,-18.6602191305988,
16.2477218462176));
#149080=CARTESIAN_POINT('Ctrl Pts',(16.2018903455192,-18.5625255464786,
16.2526163217372));
#149081=CARTESIAN_POINT('Ctrl Pts',(16.2187106399962,-18.465659449398,16.2575107972569));
#149082=CARTESIAN_POINT('Ctrl Pts',(16.2409867483463,-18.3702054253614,
16.2624052727765));
#149083=CARTESIAN_POINT('Ctrl Pts',(16.2632628566963,-18.2747514013248,
16.2672997482962));
#149084=CARTESIAN_POINT('Ctrl Pts',(16.2909946214078,-18.1807095711099,
16.2721942238158));
#149085=CARTESIAN_POINT('Ctrl Pts',(16.3239764935689,-18.088642195582,16.2770886993355));
#149086=CARTESIAN_POINT('Ctrl Pts',(16.3521750361989,-18.0099272639074,
16.2812733337285));
#149087=CARTESIAN_POINT('Ctrl Pts',(16.3842865295797,-17.9324488089606,
16.2854579681216));
#149088=CARTESIAN_POINT('Ctrl Pts',(16.4201827606336,-17.8566234515881,
16.2896426025146));
#149089=CARTESIAN_POINT('Ctrl Pts',(16.4560278978456,-17.7809060222267,
16.2938212805986));
#149090=CARTESIAN_POINT('Ctrl Pts',(16.4956468770877,-17.7068374289188,
16.2979999586825));
#149091=CARTESIAN_POINT('Ctrl Pts',(16.5388624466768,-17.6348169747563,
16.3021786367664));
#149092=CARTESIAN_POINT('Ctrl Pts',(16.5828526242923,-17.561505605713,16.3064322146519));
#149093=CARTESIAN_POINT('Ctrl Pts',(16.6305694356435,-17.4903169777092,
16.3106857925373));
#149094=CARTESIAN_POINT('Ctrl Pts',(16.6817755898823,-17.4216487427662,
16.3149393704227));
#149095=CARTESIAN_POINT('Ctrl Pts',(16.7319890129005,-17.3543117755527,
16.3191104844007));
#149096=CARTESIAN_POINT('Ctrl Pts',(16.7855574030481,-17.289398733779,16.3232815983786));
#149097=CARTESIAN_POINT('Ctrl Pts',(16.8422127801053,-17.2272562176824,
16.3274527123566));
#149098=CARTESIAN_POINT('Ctrl Pts',(16.8988491459036,-17.1651345541072,
16.331622426677));
#149099=CARTESIAN_POINT('Ctrl Pts',(16.9585701316816,-17.1057819095285,
16.3357921409973));
#149100=CARTESIAN_POINT('Ctrl Pts',(17.0210683042877,-17.0495108394989,
16.3399618553177));
#149101=CARTESIAN_POINT('Ctrl Pts',(17.0835642529406,-16.9932417718355,
16.3441314212617));
#149102=CARTESIAN_POINT('Ctrl Pts',(17.1488368494855,-16.9400543678788,
16.3483009872058));
#149103=CARTESIAN_POINT('Ctrl Pts',(17.2165437463576,-16.8902224857465,
16.3524705531498));
#149104=CARTESIAN_POINT('Ctrl Pts',(17.2866311341982,-16.8386385761127,
16.3567867158888));
#149105=CARTESIAN_POINT('Ctrl Pts',(17.3593267625534,-16.790650851497,16.3611028786277));
#149106=CARTESIAN_POINT('Ctrl Pts',(17.4342176396319,-16.7465146076938,
16.3654190413666));
#149107=CARTESIAN_POINT('Ctrl Pts',(17.5066689542667,-16.7038160973902,
16.3695946055583));
#149108=CARTESIAN_POINT('Ctrl Pts',(17.5811742544606,-16.664722174367,16.37377016975));
#149109=CARTESIAN_POINT('Ctrl Pts',(17.6573356824289,-16.6294165359951,
16.3779457339416));
#149110=CARTESIAN_POINT('Ctrl Pts',(17.7373438430673,-16.5923276937602,
16.3823321959542));
#149111=CARTESIAN_POINT('Ctrl Pts',(17.8191792885611,-16.5594201038736,
16.3867186579667));
#149112=CARTESIAN_POINT('Ctrl Pts',(17.902360657527,-16.5308482071437,16.3911051199793));
#149113=CARTESIAN_POINT('Ctrl Pts',(17.985542026493,-16.5022763104139,16.3954915819918));
#149114=CARTESIAN_POINT('Ctrl Pts',(18.0700687402227,-16.4780401936422,
16.3998780440043));
#149115=CARTESIAN_POINT('Ctrl Pts',(18.155447269861,-16.4582324209244,16.4042645060169));
#149116=CARTESIAN_POINT('Ctrl Pts',(18.2368974067893,-16.4393360331914,
16.4084491404099));
#149117=CARTESIAN_POINT('Ctrl Pts',(18.3194258684926,-16.4243990992031,
16.412633774803));
#149118=CARTESIAN_POINT('Ctrl Pts',(18.4026129434635,-16.4135393210136,
16.416818409196));
#149119=CARTESIAN_POINT('Ctrl Pts',(18.4856816119296,-16.4026950003742,
16.42099708728));
#149120=CARTESIAN_POINT('Ctrl Pts',(18.5694065793229,-16.3959163673419,
16.4251757653639));
#149121=CARTESIAN_POINT('Ctrl Pts',(18.6533561519601,-16.393270516492,16.4293544434479));
#149122=CARTESIAN_POINT('Ctrl Pts',(18.7388104603535,-16.390577240667,16.4336080213333));
#149123=CARTESIAN_POINT('Ctrl Pts',(18.8244970356235,-16.392166473525,16.4378615992187));
#149124=CARTESIAN_POINT('Ctrl Pts',(18.9099530743146,-16.3980539325116,
16.4421151771042));
#149125=CARTESIAN_POINT('Ctrl Pts',(18.993752380942,-16.4038272516174,16.4462862910821));
#149126=CARTESIAN_POINT('Ctrl Pts',(19.0773295299442,-16.4137335920112,
16.4504574050601));
#149127=CARTESIAN_POINT('Ctrl Pts',(19.1602480327619,-16.4277352328714,
16.454628519038));
#149128=CARTESIAN_POINT('Ctrl Pts',(19.2431387114752,-16.4417321753459,
16.4587982333584));
#149129=CARTESIAN_POINT('Ctrl Pts',(19.3253707297098,-16.4598216125358,
16.4629679476788));
#149130=CARTESIAN_POINT('Ctrl Pts',(19.4065148699749,-16.4819142222055,
16.4671376619991));
#149131=CARTESIAN_POINT('Ctrl Pts',(19.4876561227832,-16.5040060457254,
16.4713072279432));
#149132=CARTESIAN_POINT('Ctrl Pts',(19.5677091309388,-16.5301006368244,
16.4754767938872));
#149133=CARTESIAN_POINT('Ctrl Pts',(19.6462583168597,-16.5600583695833,
16.4796463598313));
#149134=CARTESIAN_POINT('Ctrl Pts',(19.7275691952567,-16.5910693792692,
16.4839625225702));
#149135=CARTESIAN_POINT('Ctrl Pts',(19.8072680422835,-16.626220053208,16.4882786853091));
#149136=CARTESIAN_POINT('Ctrl Pts',(19.8849166499546,-16.6653013174322,
16.492594848048));
#149137=CARTESIAN_POINT('Ctrl Pts',(19.9600358623981,-16.7031095135849,
16.4967704122397));
#149138=CARTESIAN_POINT('Ctrl Pts',(20.0332359708034,-16.7445958812711,
16.5009459764314));
#149139=CARTESIAN_POINT('Ctrl Pts',(20.1041471618793,-16.7895253169588,
16.5051215406231));
#149140=CARTESIAN_POINT('Ctrl Pts',(20.178639908641,-16.8367240316335,16.5095080026356));
#149141=CARTESIAN_POINT('Ctrl Pts',(20.2506059585104,-16.88772243629,16.5138944646482));
#149142=CARTESIAN_POINT('Ctrl Pts',(20.3196548994213,-16.9421993780623,
16.5182809266607));
#149143=CARTESIAN_POINT('Ctrl Pts',(20.3887038403321,-16.9966763198345,
16.5226673886732));
#149144=CARTESIAN_POINT('Ctrl Pts',(20.4548352860544,-17.0546313591046,
16.5270538506858));
#149145=CARTESIAN_POINT('Ctrl Pts',(20.5177042670234,-17.115699619397,16.5314403126983));
#149146=CARTESIAN_POINT('Ctrl Pts',(20.5776805529838,-17.1739580385085,
16.5356249470914));
#149147=CARTESIAN_POINT('Ctrl Pts',(20.6349112416909,-17.2352663353223,
16.5398095814844));
#149148=CARTESIAN_POINT('Ctrl Pts',(20.6890701824651,-17.2993353087707,
16.5439942158775));
#149149=CARTESIAN_POINT('Ctrl Pts',(20.7431520346907,-17.3633130879656,
16.5481728939614));
#149150=CARTESIAN_POINT('Ctrl Pts',(20.7941705292093,-17.4300433902867,
16.5523515720454));
#149151=CARTESIAN_POINT('Ctrl Pts',(20.8418355824981,-17.4991995466841,
16.5565302501293));
#149152=CARTESIAN_POINT('Ctrl Pts',(20.8903549976109,-17.5695952774834,
16.5607838280147));
#149153=CARTESIAN_POINT('Ctrl Pts',(20.9353992222982,-17.6425043486948,
16.5650374059002));
#149154=CARTESIAN_POINT('Ctrl Pts',(20.9767045339425,-17.7175461234077,
16.5692909837856));
#149155=CARTESIAN_POINT('Ctrl Pts',(21.01720906152,-17.7911330668859,16.5734620977636));
#149156=CARTESIAN_POINT('Ctrl Pts',(21.0541181225501,-17.8667703369927,
16.5776332117415));
#149157=CARTESIAN_POINT('Ctrl Pts',(21.0872271712957,-17.9440704983604,
16.5818043257195));
#149158=CARTESIAN_POINT('Ctrl Pts',(21.1203251099803,-18.0213447209124,
16.5859740400398));
#149159=CARTESIAN_POINT('Ctrl Pts',(21.149625387836,-18.1002803040063,16.5901437543602));
#149160=CARTESIAN_POINT('Ctrl Pts',(21.1749707834401,-18.1804679952253,
16.5943134686806));
#149161=CARTESIAN_POINT('Ctrl Pts',(21.2003152771464,-18.2606528330222,
16.5984830346246));
#149162=CARTESIAN_POINT('Ctrl Pts',(21.2217050305798,-18.3420892514567,
16.6026526005687));
#149163=CARTESIAN_POINT('Ctrl Pts',(21.2390325027794,-18.4243522386871,
16.6068221665127));
#149164=CARTESIAN_POINT('Ctrl Pts',(21.2569691875258,-18.5095074910661,
16.6111383292517));
#149165=CARTESIAN_POINT('Ctrl Pts',(21.2705525077454,-18.5955480019175,
16.6154544919906));
#149166=CARTESIAN_POINT('Ctrl Pts',(21.2797210678871,-18.6819921399001,
16.6197706547295));
#149167=CARTESIAN_POINT('Ctrl Pts',(21.2885909631465,-18.7656203691803,
16.6239462189212));
#149168=CARTESIAN_POINT('Ctrl Pts',(21.2933293236125,-18.8496258601582,
16.6281217831129));
#149169=CARTESIAN_POINT('Ctrl Pts',(21.2939336612287,-18.9335704012973,
16.6322973473045));
#149170=CARTESIAN_POINT('Ctrl Pts',(21.2945685225012,-19.0217547816502,
16.6366838093171));
#149171=CARTESIAN_POINT('Ctrl Pts',(21.2906407927078,-19.1098713098954,
16.6410702713296));
#149172=CARTESIAN_POINT('Ctrl Pts',(21.2822091879386,-19.197417877314,16.6454567333422));
#149173=CARTESIAN_POINT('Ctrl Pts',(21.2737775831694,-19.2849644447327,
16.6498431953547));
#149174=CARTESIAN_POINT('Ctrl Pts',(21.2608422640144,-19.3719404886095,
16.6542296573672));
#149175=CARTESIAN_POINT('Ctrl Pts',(21.2435233083642,-19.4578584434176,
16.6586161193798));
#149176=CARTESIAN_POINT('Ctrl Pts',(21.2270051786282,-19.5398035648691,
16.6627997520461));
#149177=CARTESIAN_POINT('Ctrl Pts',(21.2064383857991,-19.6210912295844,
16.6669833847125));
#149178=CARTESIAN_POINT('Ctrl Pts',(21.1818895089887,-19.7012909660358,
16.6711670173788));
#149179=CARTESIAN_POINT('Ctrl Pts',(21.1573729381804,-19.7813851606791,
16.675345144439));
#149180=CARTESIAN_POINT('Ctrl Pts',(21.1288848202252,-19.8603938336786,
16.6795232714993));
#149181=CARTESIAN_POINT('Ctrl Pts',(21.0965427533342,-19.9378964137616,
16.6837013985596));
#149182=CARTESIAN_POINT('Ctrl Pts',(21.0642335424449,-20.0153202597021,
16.6878752810998));
#149183=CARTESIAN_POINT('Ctrl Pts',(21.0280783340562,-20.0912406291167,
16.6920491636401));
#149184=CARTESIAN_POINT('Ctrl Pts',(20.9882441729195,-20.1652531511843,
16.6962230461803));
#149185=CARTESIAN_POINT('Ctrl Pts',(20.9484385271419,-20.2392126912487,
16.7003939408389));
#149186=CARTESIAN_POINT('Ctrl Pts',(20.904959378607,-20.311266693636,16.7045648354975));
#149187=CARTESIAN_POINT('Ctrl Pts',(20.8580208517639,-20.3810330371521,
16.708735730156));
#149188=CARTESIAN_POINT('Ctrl Pts',(20.8110938747831,-20.4507822137115,
16.7129055985093));
#149189=CARTESIAN_POINT('Ctrl Pts',(20.7607094614786,-20.5182444646023,
16.7170754668626));
#149190=CARTESIAN_POINT('Ctrl Pts',(20.7071258294298,-20.5830654374479,
16.7212453352159));
#149191=CARTESIAN_POINT('Ctrl Pts',(20.65354927458,-20.6478778488932,16.7254146528228));
#149192=CARTESIAN_POINT('Ctrl Pts',(20.596774638736,-20.710049325155,16.7295839704298));
#149193=CARTESIAN_POINT('Ctrl Pts',(20.5371002850679,-20.7692587493222,
16.7337532880367));
#149194=CARTESIAN_POINT('Ctrl Pts',(20.4773989743808,-20.8284949204833,
16.7379244890721));
#149195=CARTESIAN_POINT('Ctrl Pts',(20.4147956627455,-20.8847660496243,
16.7420956901075));
#149196=CARTESIAN_POINT('Ctrl Pts',(20.3496246776639,-20.9377887352192,
16.7462668911429));
#149197=CARTESIAN_POINT('Ctrl Pts',(20.3311322047064,-20.9528340898087,
16.7474504826177));
#149198=CARTESIAN_POINT('Ctrl Pts',(20.312433194898,-20.9676181441102,16.7486340740925));
#149199=CARTESIAN_POINT('Ctrl Pts',(20.2935357468249,-20.9821350335323,
16.7498176655673));
#149200=CARTESIAN_POINT('Ctrl Pts',(20.2935357468249,-20.9821350335323,
15.9499155251885));
#149201=CARTESIAN_POINT('Ctrl Pts',(20.2268602525147,-21.0333546889229,
15.954085056325));
#149202=CARTESIAN_POINT('Ctrl Pts',(20.1576411760024,-21.0812997212592,
15.9582545874615));
#149203=CARTESIAN_POINT('Ctrl Pts',(20.0862377278026,-21.1257187323817,
15.962424118598));
#149204=CARTESIAN_POINT('Ctrl Pts',(20.0148299885625,-21.1701404128959,
15.9665939003054));
#149205=CARTESIAN_POINT('Ctrl Pts',(19.9412380082957,-21.2110354095534,
15.9707636820128));
#149206=CARTESIAN_POINT('Ctrl Pts',(19.8658482018833,-21.2481967790008,
15.9749334637202));
#149207=CARTESIAN_POINT('Ctrl Pts',(19.7903802125541,-21.2853966866059,
15.9791075696952));
#149208=CARTESIAN_POINT('Ctrl Pts',(19.7131110872639,-21.3188550307645,
15.9832816756702));
#149209=CARTESIAN_POINT('Ctrl Pts',(19.6344495258896,-21.3484120370515,
15.9874557816452));
#149210=CARTESIAN_POINT('Ctrl Pts',(19.5557465373968,-21.3779846095385,
15.9916320859135));
#149211=CARTESIAN_POINT('Ctrl Pts',(19.4756500908118,-21.4036516119134,
15.9958083901818));
#149212=CARTESIAN_POINT('Ctrl Pts',(19.3945841120992,-21.4253031821518,
15.99998469445));
#149213=CARTESIAN_POINT('Ctrl Pts',(19.3133757752575,-21.4469927742223,
16.0041683326317));
#149214=CARTESIAN_POINT('Ctrl Pts',(19.2311949555798,-21.4646527513623,
16.0083519708133));
#149215=CARTESIAN_POINT('Ctrl Pts',(19.1484756590802,-21.4782244413413,
16.0125356089949));
#149216=CARTESIAN_POINT('Ctrl Pts',(19.0812407977607,-21.4892556122074,
16.0159361013208));
#149217=CARTESIAN_POINT('Ctrl Pts',(19.0136504400821,-21.4975868104144,
16.0193365936467));
#149218=CARTESIAN_POINT('Ctrl Pts',(18.9459382820314,-21.5032119011579,
16.0227370859726));
#149219=CARTESIAN_POINT('Ctrl Pts',(18.862611928595,-21.5101341188644,16.0269217203656));
#149220=CARTESIAN_POINT('Ctrl Pts',(18.7787910168742,-21.5129825827272,
16.0311063547587));
#149221=CARTESIAN_POINT('Ctrl Pts',(18.6949078655889,-21.5117015070174,
16.0352909891517));
#149222=CARTESIAN_POINT('Ctrl Pts',(18.6111441115869,-21.5104222547604,
16.0394696672357));
#149223=CARTESIAN_POINT('Ctrl Pts',(18.5273187500337,-21.5050251452316,
16.0436483453196));
#149224=CARTESIAN_POINT('Ctrl Pts',(18.4438686393695,-21.4955062008139,
16.0478270234036));
#149225=CARTESIAN_POINT('Ctrl Pts',(18.3589227454461,-21.4858166361586,
16.052080601289));
#149226=CARTESIAN_POINT('Ctrl Pts',(18.2743661679608,-21.471855975481,16.0563341791744));
#149227=CARTESIAN_POINT('Ctrl Pts',(18.1906591204414,-21.453675576209,16.0605877570599));
#149228=CARTESIAN_POINT('Ctrl Pts',(18.1085748973791,-21.435847639453,16.0647588710378));
#149229=CARTESIAN_POINT('Ctrl Pts',(18.0273080288928,-21.4139622218931,
16.0689299850158));
#149230=CARTESIAN_POINT('Ctrl Pts',(17.9472849642521,-21.3881197533225,
16.0731010989937));
#149231=CARTESIAN_POINT('Ctrl Pts',(17.8672887521235,-21.3622859564418,
16.0772708133141));
#149232=CARTESIAN_POINT('Ctrl Pts',(17.7885359523435,-21.3324978868905,
16.0814405276345));
#149233=CARTESIAN_POINT('Ctrl Pts',(17.7114383592366,-21.2989059825309,
16.0856102419549));
#149234=CARTESIAN_POINT('Ctrl Pts',(17.6343435095931,-21.2653152735154,
16.0897798078989));
#149235=CARTESIAN_POINT('Ctrl Pts',(17.5589041709151,-21.2279211833515,
16.0939493738429));
#149236=CARTESIAN_POINT('Ctrl Pts',(17.4855113682731,-21.1869219531001,
16.098118939787));
#149237=CARTESIAN_POINT('Ctrl Pts',(17.4095381652298,-21.1444812404909,
16.1024351025259));
#149238=CARTESIAN_POINT('Ctrl Pts',(17.3357585487131,-21.098177414705,16.1067512652648));
#149239=CARTESIAN_POINT('Ctrl Pts',(17.2645758959971,-21.0482807070083,
16.1110674280037));
#149240=CARTESIAN_POINT('Ctrl Pts',(17.1957120107063,-21.0000093793167,
16.1152429921954));
#149241=CARTESIAN_POINT('Ctrl Pts',(17.1292788382186,-20.948375977651,16.1194185563871));
#149242=CARTESIAN_POINT('Ctrl Pts',(17.0656083164573,-20.8936666012181,
16.1235941205788));
#149243=CARTESIAN_POINT('Ctrl Pts',(16.9987219480043,-20.8361939842407,
16.1279805825913));
#149244=CARTESIAN_POINT('Ctrl Pts',(16.9348850702689,-20.7753268941812,
16.1323670446039));
#149245=CARTESIAN_POINT('Ctrl Pts',(16.8744375629656,-20.7114395535996,
16.1367535066164));
#149246=CARTESIAN_POINT('Ctrl Pts',(16.8139900556624,-20.647552213018,16.141139968629));
#149247=CARTESIAN_POINT('Ctrl Pts',(16.7569322374057,-20.5806451127529,
16.1455264306415));
#149248=CARTESIAN_POINT('Ctrl Pts',(16.703552701499,-20.5111291697643,16.149912892654));
#149249=CARTESIAN_POINT('Ctrl Pts',(16.6525544398241,-20.4447143500982,
16.1541036735168));
#149250=CARTESIAN_POINT('Ctrl Pts',(16.6047208600206,-20.3756679864259,
16.1582944543796));
#149251=CARTESIAN_POINT('Ctrl Pts',(16.5603345705066,-20.304323408296,16.1624852352424));
#149252=CARTESIAN_POINT('Ctrl Pts',(16.516010837252,-20.2330793803581,16.1666701097864));
#149253=CARTESIAN_POINT('Ctrl Pts',(16.4751249866854,-20.1595439541278,
16.1708549843304));
#149254=CARTESIAN_POINT('Ctrl Pts',(16.437918752824,-20.0840825528056,16.1750398588744));
#149255=CARTESIAN_POINT('Ctrl Pts',(16.4007539244065,-20.0087051296905,
16.1792200762261));
#149256=CARTESIAN_POINT('Ctrl Pts',(16.3672607802463,-19.9314063968238,
16.1834002935778));
#149257=CARTESIAN_POINT('Ctrl Pts',(16.3376364602565,-19.8525785836828,
16.1875805109294));
#149258=CARTESIAN_POINT('Ctrl Pts',(16.3080359860442,-19.7738142221415,
16.1917573634601));
#149259=CARTESIAN_POINT('Ctrl Pts',(16.2822983085876,-19.6935236530688,
16.1959342159908));
#149260=CARTESIAN_POINT('Ctrl Pts',(16.2605729619717,-19.6121202068944,
16.2001110685215));
#149261=CARTESIAN_POINT('Ctrl Pts',(16.2388581016535,-19.5307560521889,
16.2042859049868));
#149262=CARTESIAN_POINT('Ctrl Pts',(16.2211518401956,-19.4482805298204,
16.2084607414521));
#149263=CARTESIAN_POINT('Ctrl Pts',(16.2075538451849,-19.3651220483341,
16.2126355779174));
#149264=CARTESIAN_POINT('Ctrl Pts',(16.1939550163507,-19.2819584676039,
16.216810670382));
#149265=CARTESIAN_POINT('Ctrl Pts',(16.1844650395067,-19.1981122945307,
16.2209857628465));
#149266=CARTESIAN_POINT('Ctrl Pts',(16.1791322578279,-19.1140210480408,
16.2251608553111));
#149267=CARTESIAN_POINT('Ctrl Pts',(16.1756711337436,-19.0594434830796,
16.2278706067979));
#149268=CARTESIAN_POINT('Ctrl Pts',(16.1739601228212,-19.0047628516759,
16.2305803582847));
#149269=CARTESIAN_POINT('Ctrl Pts',(16.174000705501,-18.9500994304892,16.2332901097715));
#149270=CARTESIAN_POINT('',(16.1740005630998,-18.9536979607663,16.1667098902285));
#149271=CARTESIAN_POINT('Ctrl Pts',(20.2954006447972,-20.9845255200926,
15.8832287071313));
#149272=CARTESIAN_POINT('Ctrl Pts',(20.2230158536215,-21.0410311268267,
15.8878110831473));
#149273=CARTESIAN_POINT('Ctrl Pts',(19.4492534979044,-21.5779135325709,
15.9347853947238));
#149274=CARTESIAN_POINT('Ctrl Pts',(17.414194801089,-21.6762257759895,16.0241516418607));
#149275=CARTESIAN_POINT('Ctrl Pts',(16.2227678370508,-20.0081650868305,
16.1140629935438));
#149276=CARTESIAN_POINT('Ctrl Pts',(16.1704459057083,-19.0564768309817,
16.1615824096664));
#149277=CARTESIAN_POINT('Ctrl Pts',(16.1712325076282,-18.9536997967236,
16.1667098902285));
#149278=CARTESIAN_POINT('Ctrl Pts',(16.1740005630998,-18.9536979607663,
16.1667098902285));
#149279=CARTESIAN_POINT('Ctrl Pts',(16.1739457994085,-18.8711312597184,
16.1708335669039));
#149280=CARTESIAN_POINT('Ctrl Pts',(16.1778897355288,-18.7884072256501,
16.1749572435793));
#149281=CARTESIAN_POINT('Ctrl Pts',(16.185851592152,-18.7059518510905,16.1790809202548));
#149282=CARTESIAN_POINT('Ctrl Pts',(16.193849980064,-18.6231181475504,16.1832235175451));
#149283=CARTESIAN_POINT('Ctrl Pts',(16.2059033176551,-18.5405560554534,
16.1873661148355));
#149284=CARTESIAN_POINT('Ctrl Pts',(16.2219780566694,-18.4586991220099,
16.1915087121259));
#149285=CARTESIAN_POINT('Ctrl Pts',(16.23794569149,-18.3773875921872,16.1956237077524));
#149286=CARTESIAN_POINT('Ctrl Pts',(16.2578812222445,-18.2967723256482,
16.1997387033789));
#149287=CARTESIAN_POINT('Ctrl Pts',(16.2816998746989,-18.2172727748012,
16.2038536990054));
#149288=CARTESIAN_POINT('Ctrl Pts',(16.3055083094402,-18.1378073276299,
16.2079669293832));
#149289=CARTESIAN_POINT('Ctrl Pts',(16.33319642467,-18.0594570997615,16.2120801597611));
#149290=CARTESIAN_POINT('Ctrl Pts',(16.3646289972004,-17.9826285278118,
16.2161933901389));
#149291=CARTESIAN_POINT('Ctrl Pts',(16.3960581246075,-17.9058083765508,
16.2203061696919));
#149292=CARTESIAN_POINT('Ctrl Pts',(16.4312307139714,-17.8305099882011,
16.2244189492448));
#149293=CARTESIAN_POINT('Ctrl Pts',(16.4699631644818,-17.7571204213743,
16.2285317287977));
#149294=CARTESIAN_POINT('Ctrl Pts',(16.5091807554343,-17.6828116189603,
16.2326960226666));
#149295=CARTESIAN_POINT('Ctrl Pts',(16.5520477937181,-17.6104602387452,
16.2368603165354));
#149296=CARTESIAN_POINT('Ctrl Pts',(16.5983263505015,-17.5404412648289,
16.2410246104042));
#149297=CARTESIAN_POINT('Ctrl Pts',(16.6440925485816,-17.4711974842891,
16.2451428005836));
#149298=CARTESIAN_POINT('Ctrl Pts',(16.6931947649454,-17.404235069768,16.2492609907631));
#149299=CARTESIAN_POINT('Ctrl Pts',(16.7453611252722,-17.3398847975652,
16.2533791809425));
#149300=CARTESIAN_POINT('Ctrl Pts',(16.7984034996616,-17.2744539105174,
16.257566526656));
#149301=CARTESIAN_POINT('Ctrl Pts',(16.8546135316781,-17.2117240820489,
16.2617538723695));
#149302=CARTESIAN_POINT('Ctrl Pts',(16.9136665630955,-17.1520038393131,
16.265941218083));
#149303=CARTESIAN_POINT('Ctrl Pts',(16.9727195945129,-17.0922835965773,
16.2701285637965));
#149304=CARTESIAN_POINT('Ctrl Pts',(17.0346152026565,-17.0355732283015,
16.27431590951));
#149305=CARTESIAN_POINT('Ctrl Pts',(17.098995528925,-16.9821369642626,16.2785032552236));
#149306=CARTESIAN_POINT('Ctrl Pts',(17.1633341687151,-16.9287353003848,
16.2826878896166));
#149307=CARTESIAN_POINT('Ctrl Pts',(17.2304115572044,-16.8783896656035,
16.2868725240096));
#149308=CARTESIAN_POINT('Ctrl Pts',(17.2999052707799,-16.8313934104547,
16.2910571584027));
#149309=CARTESIAN_POINT('Ctrl Pts',(17.3693000686557,-16.7844640486581,
16.2952358364866));
#149310=CARTESIAN_POINT('Ctrl Pts',(17.4411039821924,-16.7408748523863,
16.2994145145706));
#149311=CARTESIAN_POINT('Ctrl Pts',(17.5149611920067,-16.7008793047448,
16.3035931926545));
#149312=CARTESIAN_POINT('Ctrl Pts',(17.5901422392268,-16.6601668656561,
16.3078467705399));
#149313=CARTESIAN_POINT('Ctrl Pts',(17.6674505464318,-16.6231784826193,
16.3121003484254));
#149314=CARTESIAN_POINT('Ctrl Pts',(17.746479455157,-16.5901356572587,16.3163539263108));
#149315=CARTESIAN_POINT('Ctrl Pts',(17.8239762342742,-16.5577334315455,
16.3205250402888));
#149316=CARTESIAN_POINT('Ctrl Pts',(17.9031270518496,-16.5291253296779,
16.3246961542667));
#149317=CARTESIAN_POINT('Ctrl Pts',(17.9835248188146,-16.5044732887209,
16.3288672682447));
#149318=CARTESIAN_POINT('Ctrl Pts',(18.0638956075325,-16.4798295199942,
16.333036982565));
#149319=CARTESIAN_POINT('Ctrl Pts',(18.1455120751841,-16.4591393105014,
16.3372066968854));
#149320=CARTESIAN_POINT('Ctrl Pts',(18.2279505020323,-16.4425152111227,
16.3413764112058));
#149321=CARTESIAN_POINT('Ctrl Pts',(18.3103859953677,-16.4258917033007,
16.3455459771498));
#149322=CARTESIAN_POINT('Ctrl Pts',(18.3936429386218,-16.4133341080144,
16.3497155430939));
#149323=CARTESIAN_POINT('Ctrl Pts',(18.4772872562556,-16.404903895178,16.3538851090379));
#149324=CARTESIAN_POINT('Ctrl Pts',(18.5638724049111,-16.3961772864581,
16.3582012717768));
#149325=CARTESIAN_POINT('Ctrl Pts',(18.6508721501763,-16.3918737507556,
16.3625174345158));
#149326=CARTESIAN_POINT('Ctrl Pts',(18.7378010569179,-16.3920028218831,
16.3668335972547));
#149327=CARTESIAN_POINT('Ctrl Pts',(18.8218982636657,-16.3921276885323,
16.3710091614464));
#149328=CARTESIAN_POINT('Ctrl Pts',(18.9059287081099,-16.3964007414036,
16.3751847256381));
#149329=CARTESIAN_POINT('Ctrl Pts',(18.9894564259427,-16.4047775883436,
16.3793602898297));
#149330=CARTESIAN_POINT('Ctrl Pts',(19.0772029302351,-16.4135775299086,
16.3837467518423));
#149331=CARTESIAN_POINT('Ctrl Pts',(19.1643940106306,-16.4269066375599,
16.3881332138548));
#149332=CARTESIAN_POINT('Ctrl Pts',(19.2505367177894,-16.4446528323395,
16.3925196758674));
#149333=CARTESIAN_POINT('Ctrl Pts',(19.3366794249481,-16.462399027119,16.3969061378799));
#149334=CARTESIAN_POINT('Ctrl Pts',(19.4217732165569,-16.4845620891763,
16.4012925998925));
#149335=CARTESIAN_POINT('Ctrl Pts',(19.5053461655912,-16.510970485056,16.405679061905));
#149336=CARTESIAN_POINT('Ctrl Pts',(19.5850737993556,-16.5361637914947,
16.4098636962981));
#149337=CARTESIAN_POINT('Ctrl Pts',(19.6637142290033,-16.5653141227607,
16.4140483306911));
#149338=CARTESIAN_POINT('Ctrl Pts',(19.7408462713706,-16.5983091567015,
16.4182329650842));
#149339=CARTESIAN_POINT('Ctrl Pts',(19.817868525823,-16.6312572262956,16.4224116431681));
#149340=CARTESIAN_POINT('Ctrl Pts',(19.8933862382763,-16.6680389491569,
16.4265903212521));
#149341=CARTESIAN_POINT('Ctrl Pts',(19.96699367127,-16.7084923430913,16.430768999336));
#149342=CARTESIAN_POINT('Ctrl Pts',(20.0419204645992,-16.7496708350385,
16.4350225772214));
#149343=CARTESIAN_POINT('Ctrl Pts',(20.1148673616167,-16.7946537768954,
16.4392761551069));
#149344=CARTESIAN_POINT('Ctrl Pts',(20.1854279979956,-16.8432191278764,
16.4435297329923));
#149345=CARTESIAN_POINT('Ctrl Pts',(20.2546206787505,-16.8908429447611,
16.4477008469703));
#149346=CARTESIAN_POINT('Ctrl Pts',(20.3215184014304,-16.9419112335083,
16.4518719609482));
#149347=CARTESIAN_POINT('Ctrl Pts',(20.3857646529992,-16.9961693500964,
16.4560430749262));
#149348=CARTESIAN_POINT('Ctrl Pts',(20.4499893461177,-17.0504092598493,
16.4602127892466));
#149349=CARTESIAN_POINT('Ctrl Pts',(20.5115639839655,-17.1078365750807,
16.4643825035669));
#149350=CARTESIAN_POINT('Ctrl Pts',(20.5701645776068,-17.1681559362035,
16.4685522178873));
#149351=CARTESIAN_POINT('Ctrl Pts',(20.6287630859875,-17.2284731509046,
16.4727217838313));
#149352=CARTESIAN_POINT('Ctrl Pts',(20.6843874406312,-17.2916818763295,
16.4768913497754));
#149353=CARTESIAN_POINT('Ctrl Pts',(20.7367509982117,-17.3574503961425,
16.4810609157194));
#149354=CARTESIAN_POINT('Ctrl Pts',(20.7909555938793,-17.425531255978,16.4853770784584));
#149355=CARTESIAN_POINT('Ctrl Pts',(20.8416654983872,-17.4963548514851,
16.4896932411973));
#149356=CARTESIAN_POINT('Ctrl Pts',(20.8886099384769,-17.5695181690103,
16.4940094039362));
#149357=CARTESIAN_POINT('Ctrl Pts',(20.9340251683684,-17.6402981991626,
16.4981849681279));
#149358=CARTESIAN_POINT('Ctrl Pts',(20.9759162929431,-17.7132674273084,
16.5023605323196));
#149359=CARTESIAN_POINT('Ctrl Pts',(21.0140846597657,-17.788035247827,16.5065360965112));
#149360=CARTESIAN_POINT('Ctrl Pts',(21.0541808200598,-17.8665794132165,
16.5109225585238));
#149361=CARTESIAN_POINT('Ctrl Pts',(21.0901680280105,-17.9471081067066,
16.5153090205363));
#149362=CARTESIAN_POINT('Ctrl Pts',(21.1218737001564,-18.029146169699,16.5196954825489));
#149363=CARTESIAN_POINT('Ctrl Pts',(21.1535793723024,-18.1111842326914,
16.5240819445614));
#149364=CARTESIAN_POINT('Ctrl Pts',(21.1810033999592,-18.1947310901858,
16.5284684065739));
#149365=CARTESIAN_POINT('Ctrl Pts',(21.2040345704695,-18.2792970784325,
16.5328548685865));
#149366=CARTESIAN_POINT('Ctrl Pts',(21.2260060426843,-18.3599720602032,
16.5370395029795));
#149367=CARTESIAN_POINT('Ctrl Pts',(21.244061800264,-18.4418747378537,16.5412241373726));
#149368=CARTESIAN_POINT('Ctrl Pts',(21.2580683099057,-18.5245901651463,
16.5454087717656));
#149369=CARTESIAN_POINT('Ctrl Pts',(21.2720548830146,-18.607187857266,16.5495874498496));
#149370=CARTESIAN_POINT('Ctrl Pts',(21.2820035803663,-18.6905955514661,
16.5537661279335));
#149371=CARTESIAN_POINT('Ctrl Pts',(21.28783098536,-18.7743844088621,16.5579448060174));
#149372=CARTESIAN_POINT('Ctrl Pts',(21.2937628424001,-18.859675121309,16.5621983839029));
#149373=CARTESIAN_POINT('Ctrl Pts',(21.2954240788116,-18.9453603308621,
16.5664519617883));
#149374=CARTESIAN_POINT('Ctrl Pts',(21.2927814384536,-19.0309781629653,
16.5707055396737));
#149375=CARTESIAN_POINT('Ctrl Pts',(21.2901900308356,-19.1149361263236,
16.5748766536517));
#149376=CARTESIAN_POINT('Ctrl Pts',(21.2834601502021,-19.1988288204155,
16.5790477676297));
#149377=CARTESIAN_POINT('Ctrl Pts',(21.2726129381323,-19.2822186402176,
16.5832188816076));
#149378=CARTESIAN_POINT('Ctrl Pts',(21.2617693659493,-19.3655804777602,
16.587388595928));
#149379=CARTESIAN_POINT('Ctrl Pts',(21.2468112655211,-19.448439320332,16.5915583102483));
#149380=CARTESIAN_POINT('Ctrl Pts',(21.2278116184526,-19.5303628719679,
16.5957280245687));
#149381=CARTESIAN_POINT('Ctrl Pts',(21.208812647473,-19.6122835084123,16.5998975905128));
#149382=CARTESIAN_POINT('Ctrl Pts',(21.1857725205577,-19.6932684721469,
16.6040671564568));
#149383=CARTESIAN_POINT('Ctrl Pts',(21.1588150040537,-19.7728971897357,
16.6082367224008));
#149384=CARTESIAN_POINT('Ctrl Pts',(21.1309096945252,-19.8553255548022,
16.6125528851398));
#149385=CARTESIAN_POINT('Ctrl Pts',(21.0988065683014,-19.9363000284493,
16.6168690478787));
#149386=CARTESIAN_POINT('Ctrl Pts',(21.0626979316575,-20.0153747895704,
16.6211852106176));
#149387=CARTESIAN_POINT('Ctrl Pts',(21.0277655300544,-20.0918736986652,
16.6253607748093));
#149388=CARTESIAN_POINT('Ctrl Pts',(20.9890848280188,-20.1665943642428,
16.629536339001));
#149389=CARTESIAN_POINT('Ctrl Pts',(20.9468767362675,-20.2391583236285,
16.6337119031926));
#149390=CARTESIAN_POINT('Ctrl Pts',(20.902536814142,-20.3153873160984,16.6380983652052));
#149391=CARTESIAN_POINT('Ctrl Pts',(20.8543041199711,-20.3892355173246,
16.6424848272177));
#149392=CARTESIAN_POINT('Ctrl Pts',(20.8024847707863,-20.4603006175909,
16.6468712892303));
#149393=CARTESIAN_POINT('Ctrl Pts',(20.7506654216016,-20.5313657178571,
16.6512577512428));
#149394=CARTESIAN_POINT('Ctrl Pts',(20.6952598420585,-20.5996473145404,
16.6556442132554));
#149395=CARTESIAN_POINT('Ctrl Pts',(20.6366195645772,-20.664786849695,16.6600306752679));
#149396=CARTESIAN_POINT('Ctrl Pts',(20.5806916320421,-20.7269134235104,
16.6642142460497));
#149397=CARTESIAN_POINT('Ctrl Pts',(20.5216135032521,-20.78641336654,16.6683978168314));
#149398=CARTESIAN_POINT('Ctrl Pts',(20.4596615870938,-20.8429500487398,
16.6725813876132));
#149399=CARTESIAN_POINT('Ctrl Pts',(20.406347116845,-20.8916042865426,16.6761816775447));
#149400=CARTESIAN_POINT('Ctrl Pts',(20.3509051444086,-20.9380642575358,
16.6797819674761));
#149401=CARTESIAN_POINT('Ctrl Pts',(20.2935357468249,-20.9821350335323,
16.6833822574076));
#149402=CARTESIAN_POINT('Origin',(18.734,-18.952,-1.76670989022851));
#149403=CARTESIAN_POINT('',(20.296105573652,-20.9854858072394,17.5498940756793));
#149404=CARTESIAN_POINT('',(20.2910030417442,-20.978827659161,17.4833253052881));
#149405=CARTESIAN_POINT('',(20.2935357468249,-20.9821350335323,-1.76670989022851));
#149406=CARTESIAN_POINT('',(16.1737370593341,-18.9511644347003,17.0332901097715));
#149407=CARTESIAN_POINT('Ctrl Pts',(16.1700998810729,-18.9511632476738,
17.0332901097715));
#149408=CARTESIAN_POINT('Ctrl Pts',(16.1699051733629,-18.905425756545,17.0355745863224));
#149409=CARTESIAN_POINT('Ctrl Pts',(16.1917620149477,-18.0111494804083,
17.0802509984337));
#149410=CARTESIAN_POINT('Ctrl Pts',(17.2348044654712,-16.3222275152694,
17.1673193461055));
#149411=CARTESIAN_POINT('Ctrl Pts',(20.1337363807921,-16.2679678398935,
17.294495152787));
#149412=CARTESIAN_POINT('Ctrl Pts',(21.7484970441735,-18.6761410815923,
17.4216709594683));
#149413=CARTESIAN_POINT('Ctrl Pts',(20.9781023854704,-20.4576174664893,
17.5068039337658));
#149414=CARTESIAN_POINT('Ctrl Pts',(20.3016498302087,-20.9812337545997,
17.5495449725028));
#149415=CARTESIAN_POINT('Ctrl Pts',(20.296105573652,-20.9854858072394,17.5498940756793));
#149416=CARTESIAN_POINT('Ctrl Pts',(20.2935357468249,-20.9821350335323,
16.7498176655673));
#149417=CARTESIAN_POINT('Ctrl Pts',(20.2268584845006,-21.0333560470992,
16.7539938188206));
#149418=CARTESIAN_POINT('Ctrl Pts',(20.1577087866918,-21.081247541242,16.758169972074));
#149419=CARTESIAN_POINT('Ctrl Pts',(20.0864599732948,-21.1255804610447,
16.7623461253273));
#149420=CARTESIAN_POINT('Ctrl Pts',(20.0150847863021,-21.169992013883,16.7665296857988));
#149421=CARTESIAN_POINT('Ctrl Pts',(19.9416034481486,-21.2108321584005,
16.7707132462703));
#149422=CARTESIAN_POINT('Ctrl Pts',(19.8664139461467,-21.2479178240025,
16.7748968067418));
#149423=CARTESIAN_POINT('Ctrl Pts',(19.8011427015957,-21.2801115144034,
16.7785285131816));
#149424=CARTESIAN_POINT('Ctrl Pts',(19.7345847459897,-21.3094765936477,
16.7821602196214));
#149425=CARTESIAN_POINT('Ctrl Pts',(19.6670104728628,-21.3359235427187,
16.7857919260613));
#149426=CARTESIAN_POINT('Ctrl Pts',(19.5891480045999,-21.3663970445028,
16.7899765604543));
#149427=CARTESIAN_POINT('Ctrl Pts',(19.5096461031211,-21.3931085897472,
16.7941611948473));
#149428=CARTESIAN_POINT('Ctrl Pts',(19.4289030536307,-21.4158810332593,
16.7983458292404));
#149429=CARTESIAN_POINT('Ctrl Pts',(19.3482749318772,-21.4386210630167,
16.8025245073243));
#149430=CARTESIAN_POINT('Ctrl Pts',(19.2664096101498,-21.4574330041518,
16.8067031854083));
#149431=CARTESIAN_POINT('Ctrl Pts',(19.1837245465112,-21.4721880549406,
16.8108818634922));
#149432=CARTESIAN_POINT('Ctrl Pts',(19.0995574125316,-21.4872075794106,
16.8151354413777));
#149433=CARTESIAN_POINT('Ctrl Pts',(19.0145413088146,-21.49802316776,16.8193890192631));
#149434=CARTESIAN_POINT('Ctrl Pts',(18.9291319041929,-21.5045523579284,
16.8236425971485));
#149435=CARTESIAN_POINT('Ctrl Pts',(18.8453783275425,-21.5109549670048,
16.8278137111265));
#149436=CARTESIAN_POINT('Ctrl Pts',(18.7612470435307,-21.5132358584627,
16.8319848251044));
#149437=CARTESIAN_POINT('Ctrl Pts',(18.6771754083916,-21.5113692515517,
16.8361559390824));
#149438=CARTESIAN_POINT('Ctrl Pts',(18.5931319843017,-21.5095032709988,
16.8403256534027));
#149439=CARTESIAN_POINT('Ctrl Pts',(18.5091486288698,-21.5034925662839,
16.8444953677231));
#149440=CARTESIAN_POINT('Ctrl Pts',(18.4256629639196,-21.4933634671532,
16.8486650820435));
#149441=CARTESIAN_POINT('Ctrl Pts',(18.3421802697477,-21.4832347284594,
16.8528346479875));
#149442=CARTESIAN_POINT('Ctrl Pts',(18.2591956874268,-21.4689879429832,
16.8570042139316));
#149443=CARTESIAN_POINT('Ctrl Pts',(18.1771406148225,-21.4507011876452,
16.8611737798756));
#149444=CARTESIAN_POINT('Ctrl Pts',(18.0922005870914,-21.4317714925488,
16.8654899426145));
#149445=CARTESIAN_POINT('Ctrl Pts',(18.0082571631379,-21.4085125658604,
16.8698061053535));
#149446=CARTESIAN_POINT('Ctrl Pts',(17.9257741739147,-21.3810679311309,
16.8741222680924));
#149447=CARTESIAN_POINT('Ctrl Pts',(17.8459780593898,-21.3545173024911,
16.8782978322841));
#149448=CARTESIAN_POINT('Ctrl Pts',(17.7675491154084,-21.3240496914869,
16.8824733964757));
#149449=CARTESIAN_POINT('Ctrl Pts',(17.6908872600138,-21.2898442659165,
16.8866489606674));
#149450=CARTESIAN_POINT('Ctrl Pts',(17.6103533965495,-21.2539112056161,
16.8910354226799));
#149451=CARTESIAN_POINT('Ctrl Pts',(17.5317703445183,-21.2138530785411,
16.8954218846925));
#149452=CARTESIAN_POINT('Ctrl Pts',(17.4555708448951,-21.169931219713,16.899808346705));
#149453=CARTESIAN_POINT('Ctrl Pts',(17.3793713452718,-21.1260093608849,
16.9041948087175));
#149454=CARTESIAN_POINT('Ctrl Pts',(17.3055558437865,-21.0782241494638,
16.9085812707301));
#149455=CARTESIAN_POINT('Ctrl Pts',(17.2345184376722,-21.0268867545577,
16.9129677327426));
#149456=CARTESIAN_POINT('Ctrl Pts',(17.167299168743,-20.9783086554537,16.9171184300413));
#149457=CARTESIAN_POINT('Ctrl Pts',(17.1023079512147,-20.9263629083338,
16.9212691273401));
#149458=CARTESIAN_POINT('Ctrl Pts',(17.0399060592653,-20.8712826055498,
16.9254198246388));
#149459=CARTESIAN_POINT('Ctrl Pts',(16.9775932241692,-20.8162809106139,
16.9295645982704));
#149460=CARTESIAN_POINT('Ctrl Pts',(16.9178627255451,-20.7581538490648,
16.9337093719019));
#149461=CARTESIAN_POINT('Ctrl Pts',(16.8610458812396,-20.6971770308534,
16.9378541455334));
#149462=CARTESIAN_POINT('Ctrl Pts',(16.8042942087153,-20.6362701561228,
16.9419941649009));
#149463=CARTESIAN_POINT('Ctrl Pts',(16.7504498675423,-20.5725203603437,
16.9461341842684));
#149464=CARTESIAN_POINT('Ctrl Pts',(16.6998090154257,-20.506241628022,16.9502742036359));
#149465=CARTESIAN_POINT('Ctrl Pts',(16.6491995836852,-20.4400040186794,
16.9544116543072));
#149466=CARTESIAN_POINT('Ctrl Pts',(16.6017899801564,-20.3712409577298,
16.9585491049784));
#149467=CARTESIAN_POINT('Ctrl Pts',(16.5578367768806,-20.3003002730633,
16.9626865556497));
#149468=CARTESIAN_POINT('Ctrl Pts',(16.5138971231855,-20.2293814574863,
16.9668227308571));
#149469=CARTESIAN_POINT('Ctrl Pts',(16.4734120005631,-20.1562867489274,
16.9709589060645));
#149470=CARTESIAN_POINT('Ctrl Pts',(16.4365944037611,-20.0813925475095,
16.9750950812719));
#149471=CARTESIAN_POINT('Ctrl Pts',(16.3997766632186,-20.0064980536954,
16.9792312726275));
#149472=CARTESIAN_POINT('Ctrl Pts',(16.366626681762,-19.9298044742117,16.983367463983));
#149473=CARTESIAN_POINT('Ctrl Pts',(16.3373106052886,-19.8517110343203,
16.9875036553386));
#149474=CARTESIAN_POINT('Ctrl Pts',(16.3079666664254,-19.773543373383,16.9916437777855));
#149475=CARTESIAN_POINT('Ctrl Pts',(16.2824640727847,-19.6939736349118,
16.9957839002324));
#149476=CARTESIAN_POINT('Ctrl Pts',(16.2609198329124,-19.6134185415892,
16.9999240226793));
#149477=CARTESIAN_POINT('Ctrl Pts',(16.2393648184702,-19.532823161559,17.0040662156583));
#149478=CARTESIAN_POINT('Ctrl Pts',(16.2217721969233,-19.4512419037245,
17.0082084086373));
#149479=CARTESIAN_POINT('Ctrl Pts',(16.2082078057625,-19.3691016561093,
17.0123506016162));
#149480=CARTESIAN_POINT('Ctrl Pts',(16.1946210138151,-19.2868257587522,
17.016499635181));
#149481=CARTESIAN_POINT('Ctrl Pts',(16.1850757885661,-19.2039894937103,
17.0206486687457));
#149482=CARTESIAN_POINT('Ctrl Pts',(16.1795860271471,-19.1210244221821,
17.0247977023105));
#149483=CARTESIAN_POINT('Ctrl Pts',(16.1758404729028,-19.06441901585,17.0276285047975));
#149484=CARTESIAN_POINT('Ctrl Pts',(16.1739816679355,-19.0077536994294,
17.0304593072845));
#149485=CARTESIAN_POINT('Ctrl Pts',(16.1740001363332,-18.9511645205579,
17.0332901097715));
#149486=CARTESIAN_POINT('',(16.1741505163153,-18.9531967450726,16.9667098397546));
#149487=CARTESIAN_POINT('Ctrl Pts',(20.2935357468249,-20.9821350335323,
16.6833822574076));
#149488=CARTESIAN_POINT('Ctrl Pts',(20.2246022566296,-21.0350892658062,
16.6877082667635));
#149489=CARTESIAN_POINT('Ctrl Pts',(20.1528852371741,-21.0845926182251,
16.6920342761194));
#149490=CARTESIAN_POINT('Ctrl Pts',(20.0787695024221,-21.13034684689,16.6963602854753));
#149491=CARTESIAN_POINT('Ctrl Pts',(20.0073031503783,-21.1744655191827,
16.7005316548695));
#149492=CARTESIAN_POINT('Ctrl Pts',(19.9336070873761,-21.2150982835844,
16.7047030242637));
#149493=CARTESIAN_POINT('Ctrl Pts',(19.8580574571334,-21.2520206157908,
16.7088743936579));
#149494=CARTESIAN_POINT('Ctrl Pts',(19.7825359322864,-21.2889292124336,
16.7130442112512));
#149495=CARTESIAN_POINT('Ctrl Pts',(19.7051626224655,-21.3221299162682,
16.7172140288444));
#149496=CARTESIAN_POINT('Ctrl Pts',(19.6263379680376,-21.3514443004159,
16.7213838464377));
#149497=CARTESIAN_POINT('Ctrl Pts',(19.5475189918506,-21.3807565728622,
16.7255533636525));
#149498=CARTESIAN_POINT('Ctrl Pts',(19.4672493102343,-21.4061829222831,
16.7297228808673));
#149499=CARTESIAN_POINT('Ctrl Pts',(19.3859477373509,-21.4275936960178,
16.7338923980821));
#149500=CARTESIAN_POINT('Ctrl Pts',(19.3046276330426,-21.4490093500042,
16.7380628656733));
#149501=CARTESIAN_POINT('Ctrl Pts',(19.2222756155235,-21.4664074949664,
16.7422333332645));
#149502=CARTESIAN_POINT('Ctrl Pts',(19.1393226562911,-21.4797091494666,
16.7464038008557));
#149503=CARTESIAN_POINT('Ctrl Pts',(19.0562756364042,-21.49302588676,16.7505789973549));
#149504=CARTESIAN_POINT('Ctrl Pts',(18.9726267700264,-21.502236793061,16.7547541938541));
#149505=CARTESIAN_POINT('Ctrl Pts',(18.8888135740022,-21.5073146102397,
16.7589293903533));
#149506=CARTESIAN_POINT('Ctrl Pts',(18.8049436233579,-21.5123958658936,
16.7631074141124));
#149507=CARTESIAN_POINT('Ctrl Pts',(18.7209095809406,-21.5133384579587,
16.7672854378716));
#149508=CARTESIAN_POINT('Ctrl Pts',(18.6371480220447,-21.5101672530087,
16.7714634616307));
#149509=CARTESIAN_POINT('Ctrl Pts',(18.5532533885427,-21.5069910098663,
16.7756481231467));
#149510=CARTESIAN_POINT('Ctrl Pts',(18.4696325590993,-21.4996879708117,
16.7798327846628));
#149511=CARTESIAN_POINT('Ctrl Pts',(18.3867154767371,-21.4883346506134,
16.7840174461788));
#149512=CARTESIAN_POINT('Ctrl Pts',(18.3656523998608,-21.4854506145459,
16.7850804581023));
#149513=CARTESIAN_POINT('Ctrl Pts',(18.3446346721039,-21.4823054722714,
16.7861434700258));
#149514=CARTESIAN_POINT('Ctrl Pts',(18.3236691980734,-21.4789009939035,
16.7872064819493));
#149515=CARTESIAN_POINT('Ctrl Pts',(18.2411368748191,-21.4654989831134,
16.7913911163424));
#149516=CARTESIAN_POINT('Ctrl Pts',(18.1591082470636,-21.4480243381486,
16.7955757507354));
#149517=CARTESIAN_POINT('Ctrl Pts',(18.078016311923,-21.4265273085939,16.7997603851285));
#149518=CARTESIAN_POINT('Ctrl Pts',(17.9970398011148,-21.4050608773999,
16.8039390632124));
#149519=CARTESIAN_POINT('Ctrl Pts',(17.9169977755057,-21.3795835508678,
16.8081177412964));
#149520=CARTESIAN_POINT('Ctrl Pts',(17.838315128377,-21.3501969499492,16.8122964193803));
#149521=CARTESIAN_POINT('Ctrl Pts',(17.7582221513469,-21.320283615329,16.8165499972657));
#149522=CARTESIAN_POINT('Ctrl Pts',(17.6795382417638,-21.2863195576312,
16.8208035751512));
#149523=CARTESIAN_POINT('Ctrl Pts',(17.6026975961515,-21.2484657347861,
16.8250571530366));
#149524=CARTESIAN_POINT('Ctrl Pts',(17.5273466563966,-21.2113457821625,
16.8292282670146));
#149525=CARTESIAN_POINT('Ctrl Pts',(17.4537685795461,-21.1704857525211,
16.8333993809925));
#149526=CARTESIAN_POINT('Ctrl Pts',(17.3823529481858,-21.1260860717373,
16.8375704949705));
#149527=CARTESIAN_POINT('Ctrl Pts',(17.3109612810302,-21.0817012896951,
16.8417402092908));
#149528=CARTESIAN_POINT('Ctrl Pts',(17.241731008612,-21.0337794581183,16.8459099236112));
#149529=CARTESIAN_POINT('Ctrl Pts',(17.1750254175663,-20.9825659928516,
16.8500796379316));
#149530=CARTESIAN_POINT('Ctrl Pts',(17.1083222001917,-20.9313543499799,
16.8542492038756));
#149531=CARTESIAN_POINT('Ctrl Pts',(17.0441438499412,-20.876851587128,16.8584187698197));
#149532=CARTESIAN_POINT('Ctrl Pts',(16.9828219564699,-20.8193444941569,
16.8625883357637));
#149533=CARTESIAN_POINT('Ctrl Pts',(16.9193440608729,-20.7598155227396,
16.8669044985026));
#149534=CARTESIAN_POINT('Ctrl Pts',(16.8589276101186,-20.6970673867193,
16.8712206612416));
#149535=CARTESIAN_POINT('Ctrl Pts',(16.8018987983274,-20.6314597186284,
16.8755368239805));
#149536=CARTESIAN_POINT('Ctrl Pts',(16.7467276940819,-20.5679892134248,
16.8797123881722));
#149537=CARTESIAN_POINT('Ctrl Pts',(16.6947271674387,-20.5018430132076,
16.8838879523639));
#149538=CARTESIAN_POINT('Ctrl Pts',(16.6461502555165,-20.4333788996945,
16.8880635165555));
#149539=CARTESIAN_POINT('Ctrl Pts',(16.5951198392538,-20.3614568265659,
16.8924499785681));
#149540=CARTESIAN_POINT('Ctrl Pts',(16.5478682932595,-20.2869770238509,
16.8968364405806));
#149541=CARTESIAN_POINT('Ctrl Pts',(16.5046350837973,-20.2103847068382,
16.9012229025932));
#149542=CARTESIAN_POINT('Ctrl Pts',(16.461401874335,-20.1337923898256,16.9056093646057));
#149543=CARTESIAN_POINT('Ctrl Pts',(16.4221871920777,-20.0550881117615,
16.9099958266183));
#149544=CARTESIAN_POINT('Ctrl Pts',(16.3871718743353,-19.9747403133684,
16.9143822886308));
#149545=CARTESIAN_POINT('Ctrl Pts',(16.3503471043863,-19.8902404606612,
16.9189954255353));
#149546=CARTESIAN_POINT('Ctrl Pts',(16.3180481684136,-19.8036540013278,
16.9236085624399));
#149547=CARTESIAN_POINT('Ctrl Pts',(16.290492039707,-19.7154584782324,16.9282216993444));
#149548=CARTESIAN_POINT('Ctrl Pts',(16.2630147812854,-19.6275153855894,
16.9328216326736));
#149549=CARTESIAN_POINT('Ctrl Pts',(16.2402533773008,-19.5379726851084,
16.9374215660028));
#149550=CARTESIAN_POINT('Ctrl Pts',(16.2223767943064,-19.4473270360289,
16.9420214993319));
#149551=CARTESIAN_POINT('Ctrl Pts',(16.2045882581333,-19.3571278403507,
16.9465987767929));
#149552=CARTESIAN_POINT('Ctrl Pts',(16.1916366671696,-19.2658368103364,
16.9511760542539));
#149553=CARTESIAN_POINT('Ctrl Pts',(16.1836406660146,-19.17396231111,16.9557533317148));
#149554=CARTESIAN_POINT('Ctrl Pts',(16.1772607284146,-19.100656472263,16.9594055003442));
#149555=CARTESIAN_POINT('Ctrl Pts',(16.1740347749072,-19.0269796000837,
16.9630576689735));
#149556=CARTESIAN_POINT('Ctrl Pts',(16.1740002797795,-18.9531968587196,
16.9667098376028));
#149557=CARTESIAN_POINT('Ctrl Pts',(16.1776746515055,-18.9531940792248,
16.9667098902285));
#149558=CARTESIAN_POINT('Ctrl Pts',(16.1797896608842,-18.4498774694967,
16.9916592919231));
#149559=CARTESIAN_POINT('Ctrl Pts',(16.5671404047359,-17.0883638912152,
17.0590006291781));
#149560=CARTESIAN_POINT('Ctrl Pts',(18.7821183118115,-15.9252894968784,
17.1687339019936));
#149561=CARTESIAN_POINT('Ctrl Pts',(21.3050300753512,-17.3541588961109,
17.2959097086751));
#149562=CARTESIAN_POINT('Ctrl Pts',(21.4403822622981,-19.7410800555469,
17.4007735097732));
#149563=CARTESIAN_POINT('Ctrl Pts',(20.6127493499943,-20.732395496243,17.4632453753109));
#149564=CARTESIAN_POINT('Ctrl Pts',(20.2910030417442,-20.978827659161,17.4833253052881));
#149565=CARTESIAN_POINT('Origin',(18.734,-18.952,-1.76670989022851));
#149566=CARTESIAN_POINT('',(20.2935357468249,-20.9821350335323,18.3499540480962));
#149567=CARTESIAN_POINT('',(20.2935357468249,-20.9821350335323,18.283231855311));
#149568=CARTESIAN_POINT('',(20.2935357468249,-20.9821350335323,-1.76670989022851));
#149569=CARTESIAN_POINT('',(16.1740010840393,-18.9543559031924,17.8332901097715));
#149570=CARTESIAN_POINT('Ctrl Pts',(16.1740010840393,-18.9543559031924,
17.8332901097715));
#149571=CARTESIAN_POINT('Ctrl Pts',(16.1739248258781,-18.8714913735434,
17.837412174938));
#149572=CARTESIAN_POINT('Ctrl Pts',(16.177876160498,-18.7885152466554,17.8415342401044));
#149573=CARTESIAN_POINT('Ctrl Pts',(16.1858608731257,-18.7058557534858,
17.8456563052709));
#149574=CARTESIAN_POINT('Ctrl Pts',(16.1938402258665,-18.6232517470386,
17.8497756034244));
#149575=CARTESIAN_POINT('Ctrl Pts',(16.205847540348,-18.5409644216311,17.853894901578));
#149576=CARTESIAN_POINT('Ctrl Pts',(16.2218365582967,-18.4594202174575,
17.8580141997315));
#149577=CARTESIAN_POINT('Ctrl Pts',(16.2378199266111,-18.3779048264942,
17.862132042353));
#149578=CARTESIAN_POINT('Ctrl Pts',(16.2577821151893,-18.2971324990612,
17.8662498849744));
#149579=CARTESIAN_POINT('Ctrl Pts',(16.2816254461127,-18.2175212409839,
17.8703677275959));
#149580=CARTESIAN_POINT('Ctrl Pts',(16.3054679320359,-18.1379128043045,
17.8744854242824));
#149581=CARTESIAN_POINT('Ctrl Pts',(16.3331911499574,-18.0594658076281,
17.8786031209688));
#149582=CARTESIAN_POINT('Ctrl Pts',(16.364647494651,-17.9825833169392,17.8827208176552));
#149583=CARTESIAN_POINT('Ctrl Pts',(16.396133878009,-17.905627408714,17.8868424464612));
#149584=CARTESIAN_POINT('Ctrl Pts',(16.4313603282317,-17.8302394286303,
17.8909640752672));
#149585=CARTESIAN_POINT('Ctrl Pts',(16.470131238009,-17.7568020128526,17.8950857040732));
#149586=CARTESIAN_POINT('Ctrl Pts',(16.5089205032735,-17.683329829267,17.8992092842006));
#149587=CARTESIAN_POINT('Ctrl Pts',(16.5512573267501,-17.6118104548626,
17.903332864328));
#149588=CARTESIAN_POINT('Ctrl Pts',(16.5969016205558,-17.5425992349311,
17.9074564444553));
#149589=CARTESIAN_POINT('Ctrl Pts',(16.6426258760308,-17.4732667677586,
17.9115872484506));
#149590=CARTESIAN_POINT('Ctrl Pts',(16.691668894117,-17.4062509123682,17.915718052446));
#149591=CARTESIAN_POINT('Ctrl Pts',(16.743749207993,-17.3418752269108,17.9198488564413));
#149592=CARTESIAN_POINT('Ctrl Pts',(16.7879829276106,-17.2871985975131,
17.9233572996922));
#149593=CARTESIAN_POINT('Ctrl Pts',(16.8344068718464,-17.2344260450368,
17.9268657429432));
#149594=CARTESIAN_POINT('Ctrl Pts',(16.8828286089277,-17.1837340469049,
17.9303741861941));
#149595=CARTESIAN_POINT('Ctrl Pts',(16.9405827898754,-17.1232720517519,
17.9345588205871));
#149596=CARTESIAN_POINT('Ctrl Pts',(17.0014097311533,-17.0655300202436,
17.9387434549801));
#149597=CARTESIAN_POINT('Ctrl Pts',(17.0650229727702,-17.0108365131759,
17.9429280893731));
#149598=CARTESIAN_POINT('Ctrl Pts',(17.1285456688114,-16.9562208555457,
17.947106767457));
#149599=CARTESIAN_POINT('Ctrl Pts',(17.1948464417155,-16.9046454006956,
17.9512854455409));
#149600=CARTESIAN_POINT('Ctrl Pts',(17.2636010628235,-16.8564029572577,
17.9554641236248));
#149601=CARTESIAN_POINT('Ctrl Pts',(17.3335880611029,-16.8072958026917,
17.9597177015102));
#149602=CARTESIAN_POINT('Ctrl Pts',(17.4061174102901,-16.7616426719214,
17.9639712793957));
#149603=CARTESIAN_POINT('Ctrl Pts',(17.4808106950313,-16.7197104654835,
17.9682248572811));
#149604=CARTESIAN_POINT('Ctrl Pts',(17.5540559046947,-16.6785911966919,
17.972395971259));
#149605=CARTESIAN_POINT('Ctrl Pts',(17.6293814748148,-16.6410501005271,
17.9765670852369));
#149606=CARTESIAN_POINT('Ctrl Pts',(17.7064016963165,-16.6072949596449,
17.9807381992148));
#149607=CARTESIAN_POINT('Ctrl Pts',(17.7833960729392,-16.5735511456261,
17.9849079135351));
#149608=CARTESIAN_POINT('Ctrl Pts',(17.8620835505887,-16.5435909483339,
17.9890776278554));
#149609=CARTESIAN_POINT('Ctrl Pts',(17.9420562076481,-16.517575010448,17.9932473421758));
#149610=CARTESIAN_POINT('Ctrl Pts',(18.0220260189372,-16.4915599983208,
17.9974169081198));
#149611=CARTESIAN_POINT('Ctrl Pts',(18.1032804809781,-16.4694891080429,
18.0015864740638));
#149612=CARTESIAN_POINT('Ctrl Pts',(18.1853954972949,-16.4514734355317,
18.0057560400077));
#149613=CARTESIAN_POINT('Ctrl Pts',(18.2703975762878,-16.4328243541992,
18.0100722027467));
#149614=CARTESIAN_POINT('Ctrl Pts',(18.3563213344859,-16.4185210722995,
18.0143883654857));
#149615=CARTESIAN_POINT('Ctrl Pts',(18.4426856715119,-16.4086290160463,
18.0187045282247));
#149616=CARTESIAN_POINT('Ctrl Pts',(18.5262366993411,-16.3990591924853,
18.0228800924163));
#149617=CARTESIAN_POINT('Ctrl Pts',(18.6101995699754,-16.3936175999791,
18.0270556566079));
#149618=CARTESIAN_POINT('Ctrl Pts',(18.6941361080738,-16.3923103957471,
18.0312312207996));
#149619=CARTESIAN_POINT('Ctrl Pts',(18.7823120811748,-16.3909371677368,
18.0356176828122));
#149620=CARTESIAN_POINT('Ctrl Pts',(18.8704584082174,-16.3941269389876,
18.0400041448249));
#149621=CARTESIAN_POINT('Ctrl Pts',(18.9580725064408,-16.4018251997447,
18.0443906068375));
#149622=CARTESIAN_POINT('Ctrl Pts',(19.0456866046642,-16.4095234605017,
18.0487770688502));
#149623=CARTESIAN_POINT('Ctrl Pts',(19.1327679100281,-16.4217300548923,
18.0531635308629));
#149624=CARTESIAN_POINT('Ctrl Pts',(19.2188278686569,-16.4383289917386,
18.0575499928755));
#149625=CARTESIAN_POINT('Ctrl Pts',(19.3009280810132,-16.4541641868943,
18.0617346272685));
#149626=CARTESIAN_POINT('Ctrl Pts',(19.3824044612753,-16.4740553519454,
18.0659192616614));
#149627=CARTESIAN_POINT('Ctrl Pts',(19.4628256864494,-16.4979394630997,
18.0701038960543));
#149628=CARTESIAN_POINT('Ctrl Pts',(19.5431324419637,-16.521789578178,18.0742825741382));
#149629=CARTESIAN_POINT('Ctrl Pts',(19.6223865883779,-16.5496212203604,
18.078461252222));
#149630=CARTESIAN_POINT('Ctrl Pts',(19.7001664211471,-16.5813202564142,
18.0826399303058));
#149631=CARTESIAN_POINT('Ctrl Pts',(19.7793404015218,-16.6135874749087,
18.0868935081913));
#149632=CARTESIAN_POINT('Ctrl Pts',(19.8569862208225,-16.6498620057509,
18.0911470860768));
#149633=CARTESIAN_POINT('Ctrl Pts',(19.9326746288818,-16.689970129712,18.0954006639622));
#149634=CARTESIAN_POINT('Ctrl Pts',(20.0068956694545,-16.7293006794241,
18.0995717779401));
#149635=CARTESIAN_POINT('Ctrl Pts',(20.0792340927645,-16.7723172800336,
18.1037428919179));
#149636=CARTESIAN_POINT('Ctrl Pts',(20.1493064094736,-16.8188080800587,
18.1079140058957));
#149637=CARTESIAN_POINT('Ctrl Pts',(20.21935521274,-16.8652832796468,18.112083720216));
#149638=CARTESIAN_POINT('Ctrl Pts',(20.2871390365835,-16.9152301092314,
18.1162534345362));
#149639=CARTESIAN_POINT('Ctrl Pts',(20.3523020056982,-16.9683925241235,
18.1204231488565));
#149640=CARTESIAN_POINT('Ctrl Pts',(20.4174626560349,-17.0215530472687,
18.1245927148004));
#149641=CARTESIAN_POINT('Ctrl Pts',(20.4800022811538,-17.0779286367467,
18.1287622807444));
#149642=CARTESIAN_POINT('Ctrl Pts',(20.5395979115911,-17.1372228286486,
18.1329318466883));
#149643=CARTESIAN_POINT('Ctrl Pts',(20.601288850879,-17.1986017311943,18.1372480094273));
#149644=CARTESIAN_POINT('Ctrl Pts',(20.6598245480543,-17.2631079189011,
18.1415641721664));
#149645=CARTESIAN_POINT('Ctrl Pts',(20.7148895795158,-17.3303722764562,
18.1458803349055));
#149646=CARTESIAN_POINT('Ctrl Pts',(20.768160873366,-17.395445504635,18.150055899097));
#149647=CARTESIAN_POINT('Ctrl Pts',(20.8181839009053,-17.4630995606093,
18.1542314632886));
#149648=CARTESIAN_POINT('Ctrl Pts',(20.864716308885,-17.532969341046,18.1584070274802));
#149649=CARTESIAN_POINT('Ctrl Pts',(20.9135989581757,-17.6063680779992,
18.162793489493));
#149650=CARTESIAN_POINT('Ctrl Pts',(20.9586288003487,-17.682211752265,18.1671799515058));
#149651=CARTESIAN_POINT('Ctrl Pts',(20.9995796309652,-17.7600482661804,
18.1715664135186));
#149652=CARTESIAN_POINT('Ctrl Pts',(21.0405304615818,-17.8378847800959,
18.1759528755314));
#149653=CARTESIAN_POINT('Ctrl Pts',(21.077402106402,-17.9177135750215,18.1803393375442));
#149654=CARTESIAN_POINT('Ctrl Pts',(21.1100276507034,-17.9990610706384,
18.184725799557));
#149655=CARTESIAN_POINT('Ctrl Pts',(21.1411520453503,-18.0766656473997,
18.1889104339505));
#149656=CARTESIAN_POINT('Ctrl Pts',(21.1685283427045,-18.1559410996702,
18.193095068344));
#149657=CARTESIAN_POINT('Ctrl Pts',(21.1919760688458,-18.2364906394873,
18.1972797027375));
#149658=CARTESIAN_POINT('Ctrl Pts',(21.2153904200512,-18.3169255270044,
18.2014583808218));
#149659=CARTESIAN_POINT('Ctrl Pts',(21.2348871797097,-18.3986304619534,
18.2056370589062));
#149660=CARTESIAN_POINT('Ctrl Pts',(21.2503340551361,-18.4811890793935,
18.2098157369906));
#149661=CARTESIAN_POINT('Ctrl Pts',(21.266057804701,-18.5652275007064,18.2140693148759));
#149662=CARTESIAN_POINT('Ctrl Pts',(21.2775848741471,-18.6501500625615,
18.2183228927613));
#149663=CARTESIAN_POINT('Ctrl Pts',(21.2848289888802,-18.7355018025748,
18.2225764706466));
#149664=CARTESIAN_POINT('Ctrl Pts',(21.2919326623144,-18.8191988325688,
18.226747584625));
#149665=CARTESIAN_POINT('Ctrl Pts',(21.2949179252555,-18.9033080688144,
18.2309186986034));
#149666=CARTESIAN_POINT('Ctrl Pts',(21.2937553357682,-18.9873923862781,
18.2350898125817));
#149667=CARTESIAN_POINT('Ctrl Pts',(21.2925931363989,-19.071448488437,18.2392595269026));
#149668=CARTESIAN_POINT('Ctrl Pts',(21.287285855196,-19.1554792288143,18.2434292412234));
#149669=CARTESIAN_POINT('Ctrl Pts',(21.2778561566697,-19.2390467804621,
18.2475989555442));
#149670=CARTESIAN_POINT('Ctrl Pts',(21.2684267936926,-19.3226113584178,
18.2517685214887));
#149671=CARTESIAN_POINT('Ctrl Pts',(21.2548753574853,-19.4057123233787,
18.2559380874331));
#149672=CARTESIAN_POINT('Ctrl Pts',(21.2372763100333,-19.4879176388457,
18.2601076533776));
#149673=CARTESIAN_POINT('Ctrl Pts',(21.2190585017878,-19.5730131917741,
18.264423816116));
#149674=CARTESIAN_POINT('Ctrl Pts',(21.1965032689152,-19.6571484255578,
18.2687399788544));
#149675=CARTESIAN_POINT('Ctrl Pts',(21.1697502461668,-19.7398583237475,
18.2730561415928));
#149676=CARTESIAN_POINT('Ctrl Pts',(21.1438687003148,-19.819873955721,18.2772317057849));
#149677=CARTESIAN_POINT('Ctrl Pts',(21.1140588617648,-19.8985552629124,
18.281407269977));
#149678=CARTESIAN_POINT('Ctrl Pts',(21.0804965434243,-19.9755008410831,
18.2855828341691));
#149679=CARTESIAN_POINT('Ctrl Pts',(21.0452390721828,-20.0563327574599,
18.2899692961807));
#149680=CARTESIAN_POINT('Ctrl Pts',(21.0058403441651,-20.1352484709672,
18.2943557581922));
#149681=CARTESIAN_POINT('Ctrl Pts',(20.9625580617869,-20.2118130675798,
18.2987422202038));
#149682=CARTESIAN_POINT('Ctrl Pts',(20.9192757794087,-20.2883776641924,
18.3031286822153));
#149683=CARTESIAN_POINT('Ctrl Pts',(20.8721103180846,-20.3625906950211,
18.3075151442269));
#149684=CARTESIAN_POINT('Ctrl Pts',(20.8213695361433,-20.4340554711552,
18.3119016062384));
#149685=CARTESIAN_POINT('Ctrl Pts',(20.7729692668527,-20.5022238019799,
18.3160857345563));
#149686=CARTESIAN_POINT('Ctrl Pts',(20.7211361130876,-20.5681455333702,
18.3202698628741));
#149687=CARTESIAN_POINT('Ctrl Pts',(20.6661059352987,-20.6314542729064,
18.324453991192));
#149688=CARTESIAN_POINT('Ctrl Pts',(20.6102092801907,-20.6957598398038,
18.328704000676));
#149689=CARTESIAN_POINT('Ctrl Pts',(20.5510142592993,-20.7573689829837,
18.3329540101601));
#149690=CARTESIAN_POINT('Ctrl Pts',(20.4888142341046,-20.815927842966,18.3372040196441));
#149691=CARTESIAN_POINT('Ctrl Pts',(20.4266142089099,-20.8744867029483,
18.3414540291282));
#149692=CARTESIAN_POINT('Ctrl Pts',(20.3614094943359,-20.9299948882878,
18.3457040386122));
#149693=CARTESIAN_POINT('Ctrl Pts',(20.2935357468249,-20.9821350335323,
18.3499540480962));
#149694=CARTESIAN_POINT('Ctrl Pts',(20.296105573652,-20.9854858072394,17.5498940756793));
#149695=CARTESIAN_POINT('Ctrl Pts',(19.6284054070939,-21.4975646092715,
17.5919369080633));
#149696=CARTESIAN_POINT('Ctrl Pts',(17.7316712702996,-21.8042997980315,
17.6763716760077));
#149697=CARTESIAN_POINT('Ctrl Pts',(16.2862274700061,-20.2077259602722,
17.7708370079896));
#149698=CARTESIAN_POINT('Ctrl Pts',(16.1722336653236,-19.1559927438033,
17.8232595075876));
#149699=CARTESIAN_POINT('Ctrl Pts',(16.1740883619038,-18.9543565896946,
17.833290071625));
#149700=CARTESIAN_POINT('',(16.1740009581142,-18.9497851537726,17.7667099127478));
#149701=CARTESIAN_POINT('Ctrl Pts',(20.2910030417442,-20.978827659161,17.4833253052881));
#149702=CARTESIAN_POINT('Ctrl Pts',(19.9334915646509,-21.2526531058221,
17.5056373108713));
#149703=CARTESIAN_POINT('Ctrl Pts',(18.6971962619643,-21.7882233586031,
17.5703412520151));
#149704=CARTESIAN_POINT('Ctrl Pts',(16.6895185822271,-21.0089844641567,
17.6648027803286));
#149705=CARTESIAN_POINT('Ctrl Pts',(16.1805386002103,-19.5488856395492,
17.7369523030588));
#149706=CARTESIAN_POINT('Ctrl Pts',(16.1756126004107,-18.9497870014945,
17.7667098902285));
#149707=CARTESIAN_POINT('Ctrl Pts',(16.1740009581142,-18.9497851537726,
17.7667099127478));
#149708=CARTESIAN_POINT('Ctrl Pts',(16.1740887027229,-18.8483667747388,
17.7717442924632));
#149709=CARTESIAN_POINT('Ctrl Pts',(16.1802070184517,-18.74721232135,17.7767786721785));
#149710=CARTESIAN_POINT('Ctrl Pts',(16.1922394471764,-18.6469536230176,
17.7818130518939));
#149711=CARTESIAN_POINT('Ctrl Pts',(16.2044426849046,-18.5452716801573,
17.78691889826));
#149712=CARTESIAN_POINT('Ctrl Pts',(16.2227290670666,-18.4445110968517,
17.7920247446261));
#149713=CARTESIAN_POINT('Ctrl Pts',(16.2469282568539,-18.3453088558055,
17.7971305909922));
#149714=CARTESIAN_POINT('Ctrl Pts',(16.2587491290733,-18.2968503319625,
17.7996247057951));
#149715=CARTESIAN_POINT('Ctrl Pts',(16.2719801580747,-18.2487633198967,
17.8021188205979));
#149716=CARTESIAN_POINT('Ctrl Pts',(16.2865973915759,-18.201120201178,17.8046129354008));
#149717=CARTESIAN_POINT('Ctrl Pts',(16.3111222362101,-18.1211844127561,
17.8087975697938));
#149718=CARTESIAN_POINT('Ctrl Pts',(16.3396130703746,-18.0423026572186,
17.8129822041869));
#149719=CARTESIAN_POINT('Ctrl Pts',(16.3719611025222,-17.9648970434642,
17.8171668385799));
#149720=CARTESIAN_POINT('Ctrl Pts',(16.4042630912499,-17.8876016070201,
17.8213455166639));
#149721=CARTESIAN_POINT('Ctrl Pts',(16.440411196743,-17.8117785597319,17.8255241947478));
#149722=CARTESIAN_POINT('Ctrl Pts',(16.4802468398231,-17.7378349811527,
17.8297028728318));
#149723=CARTESIAN_POINT('Ctrl Pts',(16.5207965081759,-17.6625660170697,
17.8339564507172));
#149724=CARTESIAN_POINT('Ctrl Pts',(16.5651670712163,-17.5892450243182,
17.8382100286026));
#149725=CARTESIAN_POINT('Ctrl Pts',(16.6131398985284,-17.5182802121802,
17.8424636064881));
#149726=CARTESIAN_POINT('Ctrl Pts',(16.6601826789718,-17.448691191402,17.846634720466));
#149727=CARTESIAN_POINT('Ctrl Pts',(16.7106890267627,-17.3813682068563,
17.8508058344439));
#149728=CARTESIAN_POINT('Ctrl Pts',(16.7644072919755,-17.3166698912768,
17.8549769484219));
#149729=CARTESIAN_POINT('Ctrl Pts',(16.8181075315056,-17.2519932858419,
17.8591466627423));
#149730=CARTESIAN_POINT('Ctrl Pts',(16.875017254325,-17.1899399538654,17.8633163770626));
#149731=CARTESIAN_POINT('Ctrl Pts',(16.9348438240379,-17.130836346042,17.867486091383));
#149732=CARTESIAN_POINT('Ctrl Pts',(16.9946682648648,-17.0717348413786,
17.871655657327));
#149733=CARTESIAN_POINT('Ctrl Pts',(17.0574090183537,-17.0155831748761,
17.8758252232711));
#149734=CARTESIAN_POINT('Ctrl Pts',(17.1227367799309,-16.9626707573525,
17.8799947892151));
#149735=CARTESIAN_POINT('Ctrl Pts',(17.1903613850148,-16.9078980045032,
17.884310951954));
#149736=CARTESIAN_POINT('Ctrl Pts',(17.2607578915087,-16.8565968547187,
17.888627114693));
#149737=CARTESIAN_POINT('Ctrl Pts',(17.3335255671369,-16.8090414462952,
17.8929432774319));
#149738=CARTESIAN_POINT('Ctrl Pts',(17.4039228433851,-16.7630351502992,
17.8971188416236));
#149739=CARTESIAN_POINT('Ctrl Pts',(17.476538749062,-16.7205345053978,17.9012944058152));
#149740=CARTESIAN_POINT('Ctrl Pts',(17.5509843556046,-16.6817414276969,
17.9054699700069));
#149741=CARTESIAN_POINT('Ctrl Pts',(17.6291900327563,-16.640989003863,17.9098564320195));
#149742=CARTESIAN_POINT('Ctrl Pts',(17.7094145736834,-16.604328771398,17.914242894032));
#149743=CARTESIAN_POINT('Ctrl Pts',(17.7911842815275,-16.5719372863302,
17.9186293560446));
#149744=CARTESIAN_POINT('Ctrl Pts',(17.8729539893716,-16.5395458012624,
17.9230158180571));
#149745=CARTESIAN_POINT('Ctrl Pts',(17.9562682900626,-16.5114231770868,
17.9274022800697));
#149746=CARTESIAN_POINT('Ctrl Pts',(18.0406384682269,-16.4876847226345,
17.9317887420822));
#149747=CARTESIAN_POINT('Ctrl Pts',(18.1211266494267,-16.4650385096604,
17.9359733764752));
#149748=CARTESIAN_POINT('Ctrl Pts',(18.2028752706869,-16.4462975942589,
17.9401580108683));
#149749=CARTESIAN_POINT('Ctrl Pts',(18.2854705184226,-16.4315989794963,
17.9443426452613));
#149750=CARTESIAN_POINT('Ctrl Pts',(18.3679482020464,-16.4169212863925,
17.9485213233452));
#149751=CARTESIAN_POINT('Ctrl Pts',(18.4512696694584,-16.4062745451513,
17.9527000014292));
#149752=CARTESIAN_POINT('Ctrl Pts',(18.5350067952746,-16.3997457602204,
17.9568786795131));
#149753=CARTESIAN_POINT('Ctrl Pts',(18.6202448488908,-16.3930999515116,
17.9611322573985));
#149754=CARTESIAN_POINT('Ctrl Pts',(18.7059131447157,-16.3907213105009,
17.965385835284));
#149755=CARTESIAN_POINT('Ctrl Pts',(18.7915501028463,-16.3926469595497,
17.9696394131694));
#149756=CARTESIAN_POINT('Ctrl Pts',(18.8755268214363,-16.394535276134,17.9738105271473));
#149757=CARTESIAN_POINT('Ctrl Pts',(18.9594729254762,-16.40056246717,17.9779816411253));
#149758=CARTESIAN_POINT('Ctrl Pts',(19.0429506482601,-16.4107110559915,
17.9821527551032));
#149759=CARTESIAN_POINT('Ctrl Pts',(19.126400359288,-16.4208562393561,17.9863224694236));
#149760=CARTESIAN_POINT('Ctrl Pts',(19.2093815449112,-16.4351200184238,
17.9904921837439));
#149761=CARTESIAN_POINT('Ctrl Pts',(19.2914613132267,-16.4534330338661,
17.9946618980643));
#149762=CARTESIAN_POINT('Ctrl Pts',(19.3735381607919,-16.4717453976528,
17.9988314640083));
#149763=CARTESIAN_POINT('Ctrl Pts',(19.4547132060174,-16.4941066103199,
18.0030010299523));
#149764=CARTESIAN_POINT('Ctrl Pts',(19.5345648538857,-16.5203964314216,
18.0071705958964));
#149765=CARTESIAN_POINT('Ctrl Pts',(19.6172239871861,-16.5476105702015,
18.0114867586353));
#149766=CARTESIAN_POINT('Ctrl Pts',(19.6984644293621,-16.5790345522992,
18.0158029213743));
#149767=CARTESIAN_POINT('Ctrl Pts',(19.7778387647095,-16.6144798111482,
18.0201190841132));
#149768=CARTESIAN_POINT('Ctrl Pts',(19.854627489431,-16.6487704444181,18.0242946483049));
#149769=CARTESIAN_POINT('Ctrl Pts',(19.9296694183934,-16.6868241363793,
18.0284702124965));
#149770=CARTESIAN_POINT('Ctrl Pts',(20.0025842524509,-16.7284231530182,
18.0326457766882));
#149771=CARTESIAN_POINT('Ctrl Pts',(20.0791818414392,-16.7721232370959,
18.0370322387008));
#149772=CARTESIAN_POINT('Ctrl Pts',(20.1534313177604,-16.81973589169,18.0414187007134));
#149773=CARTESIAN_POINT('Ctrl Pts',(20.2249278226101,-16.8709583791363,
18.0458051627259));
#149774=CARTESIAN_POINT('Ctrl Pts',(20.2964243274599,-16.9221808665826,
18.0501916247385));
#149775=CARTESIAN_POINT('Ctrl Pts',(20.3651674546736,-16.9770127656117,
18.0545780867511));
#149776=CARTESIAN_POINT('Ctrl Pts',(20.43079571541,-17.0351055584184,18.0589645487637));
#149777=CARTESIAN_POINT('Ctrl Pts',(20.4934043225857,-17.0905254157142,
18.0631491831568));
#149778=CARTESIAN_POINT('Ctrl Pts',(20.5534114448282,-17.1491189671382,
18.0673338175499));
#149779=CARTESIAN_POINT('Ctrl Pts',(20.6104778947948,-17.2106124181141,
18.071518451943));
#149780=CARTESIAN_POINT('Ctrl Pts',(20.6674631177333,-17.2720183407739,
18.075697130027));
#149781=CARTESIAN_POINT('Ctrl Pts',(20.721515672228,-17.3363156298581,18.079875808111));
#149782=CARTESIAN_POINT('Ctrl Pts',(20.7723306651571,-17.4031913935285,
18.084054486195));
#149783=CARTESIAN_POINT('Ctrl Pts',(20.8240564803134,-17.4712658571987,
18.0883080640804));
#149784=CARTESIAN_POINT('Ctrl Pts',(20.8724271646771,-17.5420118234208,
18.0925616419659));
#149785=CARTESIAN_POINT('Ctrl Pts',(20.9171616597699,-17.6150612701732,
18.0968152198513));
#149786=CARTESIAN_POINT('Ctrl Pts',(20.9610288893838,-17.6866945108573,
18.1009863338293));
#149787=CARTESIAN_POINT('Ctrl Pts',(21.0013994094996,-17.7605423037904,
18.1051574478073));
#149788=CARTESIAN_POINT('Ctrl Pts',(21.0380509604127,-17.8362270966629,
18.1093285617853));
#149789=CARTESIAN_POINT('Ctrl Pts',(21.0746902125439,-17.9118864927723,
18.1134982761058));
#149790=CARTESIAN_POINT('Ctrl Pts',(21.1076127735552,-17.9893812509009,
18.1176679904262));
#149791=CARTESIAN_POINT('Ctrl Pts',(21.136642647489,-18.068309834576,18.1218377047466));
#149792=CARTESIAN_POINT('Ctrl Pts',(21.1656714884152,-18.1472356096333,
18.1260072706907));
#149793=CARTESIAN_POINT('Ctrl Pts',(21.1908077596747,-18.2275946767429,
18.1301768366348));
#149794=CARTESIAN_POINT('Ctrl Pts',(21.2119243630671,-18.3089674573408,
18.1343464025789));
#149795=CARTESIAN_POINT('Ctrl Pts',(21.2337834001839,-18.3932012045179,
18.1386625653178));
#149796=CARTESIAN_POINT('Ctrl Pts',(21.2513347146948,-18.478520765314,18.1429787280566));
#149797=CARTESIAN_POINT('Ctrl Pts',(21.264494683606,-18.5644478664209,18.1472948907955));
#149798=CARTESIAN_POINT('Ctrl Pts',(21.2772259679145,-18.6475759012496,
18.1514704549872));
#149799=CARTESIAN_POINT('Ctrl Pts',(21.2858476079666,-18.731272029579,18.1556460191789));
#149800=CARTESIAN_POINT('Ctrl Pts',(21.290336834896,-18.8150986247191,18.1598215833707));
#149801=CARTESIAN_POINT('Ctrl Pts',(21.2950528020053,-18.9031591018971,
18.1642080453831));
#149802=CARTESIAN_POINT('Ctrl Pts',(21.295207927637,-18.9913629881317,18.1685945073955));
#149803=CARTESIAN_POINT('Ctrl Pts',(21.2908376238656,-19.0792059950831,
18.1729809694079));
#149804=CARTESIAN_POINT('Ctrl Pts',(21.2864673200943,-19.1670490020345,
18.1773674314203));
#149805=CARTESIAN_POINT('Ctrl Pts',(21.2775717212915,-19.2545305601574,
18.1817538934327));
#149806=CARTESIAN_POINT('Ctrl Pts',(21.2642482087235,-19.3411580684654,
18.1861403554451));
#149807=CARTESIAN_POINT('Ctrl Pts',(21.2515412573713,-19.4237767869309,
18.1903238287684));
#149808=CARTESIAN_POINT('Ctrl Pts',(21.234759861393,-19.5059261893835,18.1945073020916));
#149809=CARTESIAN_POINT('Ctrl Pts',(21.2139505970119,-19.5871732333625,
18.1986907754148));
#149810=CARTESIAN_POINT('Ctrl Pts',(21.1931684634955,-19.6683143484382,
18.2028687943766));
#149811=CARTESIAN_POINT('Ctrl Pts',(21.1683689994537,-19.7485549992071,
18.2070468133384));
#149812=CARTESIAN_POINT('Ctrl Pts',(21.1396501998678,-19.8274696544575,
18.2112248323002));
#149813=CARTESIAN_POINT('Ctrl Pts',(21.1109602255684,-19.9063051024438,
18.2153986577513));
#149814=CARTESIAN_POINT('Ctrl Pts',(21.0783588838323,-19.9838167679928,
18.2195724832024));
#149815=CARTESIAN_POINT('Ctrl Pts',(21.0419943136806,-20.0595929974581,
18.2237463086536));
#149816=CARTESIAN_POINT('Ctrl Pts',(21.0056553325342,-20.1353159047383,
18.2279171970689));
#149817=CARTESIAN_POINT('Ctrl Pts',(20.9655585822445,-20.2093053885048,
18.2320880854843));
#149818=CARTESIAN_POINT('Ctrl Pts',(20.9219002659528,-20.2811698259604,
18.2362589738997));
#149819=CARTESIAN_POINT('Ctrl Pts',(20.8782487043936,-20.3530231446856,
18.240429217003));
#149820=CARTESIAN_POINT('Ctrl Pts',(20.8310368995146,-20.4227516709466,
18.2445994601064));
#149821=CARTESIAN_POINT('Ctrl Pts',(20.7805064538477,-20.4899893804444,
18.2487697032098));
#149822=CARTESIAN_POINT('Ctrl Pts',(20.7299824361662,-20.5572185366233,
18.2529394158159));
#149823=CARTESIAN_POINT('Ctrl Pts',(20.6761408980474,-20.6219571415484,
18.257109128422));
#149824=CARTESIAN_POINT('Ctrl Pts',(20.6192651021132,-20.6838705190499,
18.2612788410281));
#149825=CARTESIAN_POINT('Ctrl Pts',(20.5623509461028,-20.7458256542418,
18.2654513659113));
#149826=CARTESIAN_POINT('Ctrl Pts',(20.5023987594139,-20.8049514195305,
18.2696238907944));
#149827=CARTESIAN_POINT('Ctrl Pts',(20.4397297081187,-20.8609489681082,
18.2737964156776));
#149828=CARTESIAN_POINT('Ctrl Pts',(20.392491319937,-20.9031585417695,18.276941562222));
#149829=CARTESIAN_POINT('Ctrl Pts',(20.3437100762383,-20.9435914593361,
18.2800867087665));
#149830=CARTESIAN_POINT('Ctrl Pts',(20.2935357468249,-20.9821350335323,
18.283231855311));
#149831=CARTESIAN_POINT('Origin',(18.734,-18.952,-1.76670989022851));
#149832=CARTESIAN_POINT('',(20.2912840470176,-20.9792340293575,19.149828721203));
#149833=CARTESIAN_POINT('',(20.2935357468249,-20.9821350335323,19.0833436973871));
#149834=CARTESIAN_POINT('',(20.2935357468249,-20.9821350335323,-1.76670989022851));
#149835=CARTESIAN_POINT('',(16.1743944468539,-18.9516176052701,18.6332901348849));
#149836=CARTESIAN_POINT('Ctrl Pts',(16.178162963747,-18.9516133246024,18.6332903748342));
#149837=CARTESIAN_POINT('Ctrl Pts',(16.1776269370726,-18.5470182282415,
18.6533365919837));
#149838=CARTESIAN_POINT('Ctrl Pts',(16.4590847030962,-17.2875284349863,
18.7157747446936));
#149839=CARTESIAN_POINT('Ctrl Pts',(18.4329096448176,-15.9399184650897,
18.8206048329641));
#149840=CARTESIAN_POINT('Ctrl Pts',(21.1037093988242,-17.0684480546079,
18.9477806396456));
#149841=CARTESIAN_POINT('Ctrl Pts',(21.532350067299,-19.5334127108451,19.0575219357252));
#149842=CARTESIAN_POINT('Ctrl Pts',(20.689118793848,-20.6706543549497,19.1248712962443));
#149843=CARTESIAN_POINT('Ctrl Pts',(20.2912840470176,-20.9792340293575,
19.149828721203));
#149844=CARTESIAN_POINT('Ctrl Pts',(20.2935357468249,-20.9821350335323,
18.3499540480962));
#149845=CARTESIAN_POINT('Ctrl Pts',(20.2269224998199,-21.0333068709719,
18.3541251295808));
#149846=CARTESIAN_POINT('Ctrl Pts',(20.1577388901063,-21.0812344067916,
18.3582962110655));
#149847=CARTESIAN_POINT('Ctrl Pts',(20.0863370407774,-21.1256569481271,
18.3624672925501));
#149848=CARTESIAN_POINT('Ctrl Pts',(20.0149588057502,-21.1700647978644,
18.3666369945581));
#149849=CARTESIAN_POINT('Ctrl Pts',(19.9413641784025,-21.2109697124809,
18.3708066965662));
#149850=CARTESIAN_POINT('Ctrl Pts',(19.8659339889943,-21.2481544905689,
18.3749763985743));
#149851=CARTESIAN_POINT('Ctrl Pts',(19.7905061189634,-21.2853381252747,
18.3791459723696));
#149852=CARTESIAN_POINT('Ctrl Pts',(19.7132432121151,-21.3188016482936,
18.3833155461649));
#149853=CARTESIAN_POINT('Ctrl Pts',(19.6345491728624,-21.3483745924327,
18.3874851199602));
#149854=CARTESIAN_POINT('Ctrl Pts',(19.5534056690215,-21.3788680367789,
18.3917844777068));
#149855=CARTESIAN_POINT('Ctrl Pts',(19.4707409474977,-21.4052244983156,
18.3960838354535));
#149856=CARTESIAN_POINT('Ctrl Pts',(19.3870163747539,-21.4273120236251,
18.4003831932001));
#149857=CARTESIAN_POINT('Ctrl Pts',(19.3057019498923,-21.4487637236256,
18.4045587869474));
#149858=CARTESIAN_POINT('Ctrl Pts',(19.2233883403865,-21.4661889020904,
18.4087343806946));
#149859=CARTESIAN_POINT('Ctrl Pts',(19.1405083157769,-21.4795187416129,
18.4129099744419));
#149860=CARTESIAN_POINT('Ctrl Pts',(19.0539434631163,-21.4934412229307,
18.4172712141882));
#149861=CARTESIAN_POINT('Ctrl Pts',(18.9667612220343,-21.5028956728378,
18.4216324539346));
#149862=CARTESIAN_POINT('Ctrl Pts',(18.8794581082821,-21.5078642254109,
18.4259936936809));
#149863=CARTESIAN_POINT('Ctrl Pts',(18.7921549945299,-21.5128327779839,
18.4303549334272));
#149864=CARTESIAN_POINT('Ctrl Pts',(18.7047315721785,-21.5133155043339,
18.4347161731735));
#149865=CARTESIAN_POINT('Ctrl Pts',(18.6176794289205,-21.5093559636358,
18.4390774129198));
#149866=CARTESIAN_POINT('Ctrl Pts',(18.5341524013308,-21.5055567617695,
18.4432620473123));
#149867=CARTESIAN_POINT('Ctrl Pts',(18.4506562604967,-21.4976540121365,
18.4474466817048));
#149868=CARTESIAN_POINT('Ctrl Pts',(18.3676269095302,-21.4856477179315,
18.4516313160972));
#149869=CARTESIAN_POINT('Ctrl Pts',(18.2847157405684,-21.4736585132003,
18.4558099941806));
#149870=CARTESIAN_POINT('Ctrl Pts',(18.2022704931349,-21.4575774310126,
18.4599886722639));
#149871=CARTESIAN_POINT('Ctrl Pts',(18.1207249420864,-21.4374564376269,
18.4641673503473));
#149872=CARTESIAN_POINT('Ctrl Pts',(18.0377177456262,-21.4169747898918,
18.4684209282328));
#149873=CARTESIAN_POINT('Ctrl Pts',(17.9556432985578,-21.392306997499,18.4726745061184));
#149874=CARTESIAN_POINT('Ctrl Pts',(17.8749514567217,-21.3635628957777,
18.476928084004));
#149875=CARTESIAN_POINT('Ctrl Pts',(17.7958239837111,-21.3353760545627,
18.4810991979814));
#149876=CARTESIAN_POINT('Ctrl Pts',(17.7180264386452,-21.3032697094724,
18.4852703119587));
#149877=CARTESIAN_POINT('Ctrl Pts',(17.6419689102695,-21.2673980433312,
18.4894414259361));
#149878=CARTESIAN_POINT('Ctrl Pts',(17.565936903732,-21.231538414274,18.4936111402558));
#149879=CARTESIAN_POINT('Ctrl Pts',(17.4916441700225,-21.1919161695519,
18.4977808545756));
#149880=CARTESIAN_POINT('Ctrl Pts',(17.4194798631978,-21.1487332131921,
18.5019505688953));
#149881=CARTESIAN_POINT('Ctrl Pts',(17.3473181242889,-21.1055517934673,
18.5061201348388));
#149882=CARTESIAN_POINT('Ctrl Pts',(17.2772850559933,-21.0588101509786,
18.5102897007822));
#149883=CARTESIAN_POINT('Ctrl Pts',(17.209743095842,-21.0087549416804,18.5144592667256));
#149884=CARTESIAN_POINT('Ctrl Pts',(17.1398264436719,-20.9569398529568,
18.5187754294653));
#149885=CARTESIAN_POINT('Ctrl Pts',(17.0725797574073,-20.9015741660661,
18.5230915922049));
#149886=CARTESIAN_POINT('Ctrl Pts',(17.008368511561,-20.8429775160239,18.5274077549446));
#149887=CARTESIAN_POINT('Ctrl Pts',(16.9462489403138,-20.7862896457112,
18.5315833191356));
#149888=CARTESIAN_POINT('Ctrl Pts',(16.8869703858408,-20.7265784444842,
18.5357588833267));
#149889=CARTESIAN_POINT('Ctrl Pts',(16.8308254399577,-20.6641701416646,
18.5399344475178));
#149890=CARTESIAN_POINT('Ctrl Pts',(16.7718447463026,-20.5986097438008,
18.5443209095317));
#149891=CARTESIAN_POINT('Ctrl Pts',(16.7163229051915,-20.5300730764181,
18.5487073715456));
#149892=CARTESIAN_POINT('Ctrl Pts',(16.6645491064846,-20.4589747839059,
18.5530938335595));
#149893=CARTESIAN_POINT('Ctrl Pts',(16.6127753077778,-20.3878764913938,
18.5574802955735));
#149894=CARTESIAN_POINT('Ctrl Pts',(16.5647498046499,-20.314217101332,18.5618667575874));
#149895=CARTESIAN_POINT('Ctrl Pts',(16.5207062260026,-20.2384410868689,
18.5662532196013));
#149896=CARTESIAN_POINT('Ctrl Pts',(16.4770273612297,-20.1632925546556,
18.5706033584189));
#149897=CARTESIAN_POINT('Ctrl Pts',(16.4371122169919,-20.0858014915384,
18.5749534972364));
#149898=CARTESIAN_POINT('Ctrl Pts',(16.4012086273382,-20.0063644586359,
18.579303636054));
#149899=CARTESIAN_POINT('Ctrl Pts',(16.3640774712897,-19.924211423433,18.5838025088638));
#149900=CARTESIAN_POINT('Ctrl Pts',(16.3312374248383,-19.8399772763342,
18.5883013816736));
#149901=CARTESIAN_POINT('Ctrl Pts',(16.3029130373491,-19.7541322709061,
18.5928002544834));
#149902=CARTESIAN_POINT('Ctrl Pts',(16.2756354411693,-19.6714598603193,
18.5971328613515));
#149903=CARTESIAN_POINT('Ctrl Pts',(16.252545805577,-19.5872939815205,18.6014654682196));
#149904=CARTESIAN_POINT('Ctrl Pts',(16.2337970621825,-19.5020775124732,
18.6057980750876));
#149905=CARTESIAN_POINT('Ctrl Pts',(16.2150725182341,-19.416971034336,18.6101250897577));
#149906=CARTESIAN_POINT('Ctrl Pts',(16.2006778102741,-19.3308170607077,
18.6144521044277));
#149907=CARTESIAN_POINT('Ctrl Pts',(16.190716084581,-19.244073493441,18.6187791190978));
#149908=CARTESIAN_POINT('Ctrl Pts',(16.180768168227,-19.1574501735471,18.6231001354885));
#149909=CARTESIAN_POINT('Ctrl Pts',(16.1752410444518,-19.0702392928349,
18.6274211518792));
#149910=CARTESIAN_POINT('Ctrl Pts',(16.1741865858058,-18.9829076772249,
18.6317421682699));
#149911=CARTESIAN_POINT('Ctrl Pts',(16.1740606709629,-18.9724792486655,
18.6322581487704));
#149912=CARTESIAN_POINT('Ctrl Pts',(16.1739984722012,-18.9620491070313,
18.632774129271));
#149913=CARTESIAN_POINT('Ctrl Pts',(16.1740000284928,-18.9516180532909,
18.6332901097715));
#149914=CARTESIAN_POINT('',(16.1740000028035,-18.9518801919504,18.5667098901964));
#149915=CARTESIAN_POINT('Ctrl Pts',(20.2935357468249,-20.9821350335323,
18.283231855311));
#149916=CARTESIAN_POINT('Ctrl Pts',(20.2268916049204,-21.0333306042209,
18.2874094017789));
#149917=CARTESIAN_POINT('Ctrl Pts',(20.1577889841688,-21.0811911374411,
18.2915869482468));
#149918=CARTESIAN_POINT('Ctrl Pts',(20.086602957854,-21.1254914856987,18.2957644947147));
#149919=CARTESIAN_POINT('Ctrl Pts',(20.0153008952338,-21.1698640454422,
18.2999488507643));
#149920=CARTESIAN_POINT('Ctrl Pts',(19.9419090508425,-21.2106646154573,
18.3041332068138));
#149921=CARTESIAN_POINT('Ctrl Pts',(19.8668262210657,-21.247714431907,18.3083175628634));
#149922=CARTESIAN_POINT('Ctrl Pts',(19.8369284324813,-21.2624675729726,
18.3099837626177));
#149923=CARTESIAN_POINT('Ctrl Pts',(19.8067627272952,-21.2766265326087,
18.3116499623721));
#149924=CARTESIAN_POINT('Ctrl Pts',(19.7763550154486,-21.2901822045703,
18.3133161621265));
#149925=CARTESIAN_POINT('Ctrl Pts',(19.6999865269343,-21.3242270608135,
18.3175007965194));
#149926=CARTESIAN_POINT('Ctrl Pts',(19.6218062328674,-21.3545898770089,
18.3216854309123));
#149927=CARTESIAN_POINT('Ctrl Pts',(19.5422037920528,-21.3810752624222,
18.3258700653053));
#149928=CARTESIAN_POINT('Ctrl Pts',(19.4627146554598,-21.4075229491676,
18.3300487433891));
#149929=CARTESIAN_POINT('Ctrl Pts',(19.3818078256885,-21.4301040236941,
18.3342274214729));
#149930=CARTESIAN_POINT('Ctrl Pts',(19.2998943515241,-21.4486704994679,
18.3384060995568));
#149931=CARTESIAN_POINT('Ctrl Pts',(19.2165126372027,-21.467569765977,18.3426596774422));
#149932=CARTESIAN_POINT('Ctrl Pts',(19.1320882756879,-21.4823088984316,
18.3469132553277));
#149933=CARTESIAN_POINT('Ctrl Pts',(19.0470726305021,-21.4927844316334,
18.3511668332132));
#149934=CARTESIAN_POINT('Ctrl Pts',(18.9637051794954,-21.5030568761824,
18.355337947191));
#149935=CARTESIAN_POINT('Ctrl Pts',(18.8797696442091,-21.5092295037566,
18.3595090611688));
#149936=CARTESIAN_POINT('Ctrl Pts',(18.7957017187999,-21.5112563173502,
18.3636801751467));
#149937=CARTESIAN_POINT('Ctrl Pts',(18.7116620031949,-21.513282450827,18.3678498894669));
#149938=CARTESIAN_POINT('Ctrl Pts',(18.6274904452119,-21.5111655221263,
18.3720196037872));
#149939=CARTESIAN_POINT('Ctrl Pts',(18.5436254163484,-21.5049115765924,
18.3761893181075));
#149940=CARTESIAN_POINT('Ctrl Pts',(18.4597633717625,-21.4986578536007,
18.3803588840514));
#149941=CARTESIAN_POINT('Ctrl Pts',(18.3762082933047,-21.4882674415331,
18.3845284499953));
#149942=CARTESIAN_POINT('Ctrl Pts',(18.2933947304044,-21.4737983655329,
18.3886980159393));
#149943=CARTESIAN_POINT('Ctrl Pts',(18.2076695447891,-21.4588205746693,
18.3930141786783));
#149944=CARTESIAN_POINT('Ctrl Pts',(18.1227395078358,-21.4394720625982,
18.3973303414174));
#149945=CARTESIAN_POINT('Ctrl Pts',(18.0390745966241,-21.415874729718,18.4016465041564));
#149946=CARTESIAN_POINT('Ctrl Pts',(17.9581350610998,-21.3930460774757,
18.405822068348));
#149947=CARTESIAN_POINT('Ctrl Pts',(17.878379925585,-21.3662413589922,18.4099976325396));
#149948=CARTESIAN_POINT('Ctrl Pts',(17.8002169726158,-21.3356210390432,
18.4141731967311));
#149949=CARTESIAN_POINT('Ctrl Pts',(17.7181061946998,-21.3034541595236,
18.4185596587439));
#149950=CARTESIAN_POINT('Ctrl Pts',(17.6377532005344,-21.2670763374213,
18.4229461207567));
#149951=CARTESIAN_POINT('Ctrl Pts',(17.559602363678,-21.2267285973938,18.4273325827695));
#149952=CARTESIAN_POINT('Ctrl Pts',(17.4814515268215,-21.1863808573663,
18.4317190447823));
#149953=CARTESIAN_POINT('Ctrl Pts',(17.4055033100765,-21.1420635575358,
18.4361055067951));
#149954=CARTESIAN_POINT('Ctrl Pts',(17.3321657913464,-21.0940692919344,
18.4404919688079));
#149955=CARTESIAN_POINT('Ctrl Pts',(17.2622960528831,-21.0483444454524,
18.4446710160258));
#149956=CARTESIAN_POINT('Ctrl Pts',(17.19453408493,-20.9991112651902,18.4488500632436));
#149957=CARTESIAN_POINT('Ctrl Pts',(17.1292545139165,-20.9465906660001,
18.4530291104615));
#149958=CARTESIAN_POINT('Ctrl Pts',(17.0640679209105,-20.8941448721524,
18.4572022054423));
#149959=CARTESIAN_POINT('Ctrl Pts',(17.0013570587501,-20.8384212459578,
18.461375300423));
#149960=CARTESIAN_POINT('Ctrl Pts',(16.9414683281885,-20.7796843834625,
18.4655483954038));
#149961=CARTESIAN_POINT('Ctrl Pts',(16.8809773183908,-20.7203568256503,
18.4697634576868));
#149962=CARTESIAN_POINT('Ctrl Pts',(16.8233659292103,-20.6579553356915,
18.4739785199699));
#149963=CARTESIAN_POINT('Ctrl Pts',(16.7689574885196,-20.5927949073772,
18.4781935822529));
#149964=CARTESIAN_POINT('Ctrl Pts',(16.715187711247,-20.5283993526991,18.4823591668069));
#149965=CARTESIAN_POINT('Ctrl Pts',(16.6645463875622,-20.4613096522779,
18.4865247513609));
#149966=CARTESIAN_POINT('Ctrl Pts',(16.6173078768047,-20.3918661241945,
18.4906903359149));
#149967=CARTESIAN_POINT('Ctrl Pts',(16.5700850499656,-20.3224456524398,
18.4948545374302));
#149968=CARTESIAN_POINT('Ctrl Pts',(16.5262630517185,-20.2506732862345,
18.4990187389455));
#149969=CARTESIAN_POINT('Ctrl Pts',(16.4860739671284,-20.1769198140034,
18.5031829404608));
#149970=CARTESIAN_POINT('Ctrl Pts',(16.4458860826634,-20.1031685441962,
18.5073470176248));
#149971=CARTESIAN_POINT('Ctrl Pts',(16.4093311160888,-20.0274366916313,
18.5115110947889));
#149972=CARTESIAN_POINT('Ctrl Pts',(16.3765953977372,-19.9501200034215,
18.5156751719529));
#149973=CARTESIAN_POINT('Ctrl Pts',(16.3431614559385,-19.8711542197504,
18.5199280651399));
#149974=CARTESIAN_POINT('Ctrl Pts',(16.313711777103,-19.7905356687049,18.5241809583268));
#149975=CARTESIAN_POINT('Ctrl Pts',(16.2883925214925,-19.7087060598861,
18.5284338515138));
#149976=CARTESIAN_POINT('Ctrl Pts',(16.2635663208297,-19.6284699613234,
18.5326039259141));
#149977=CARTESIAN_POINT('Ctrl Pts',(16.2427111716313,-19.5470700198228,
18.5367740003145));
#149978=CARTESIAN_POINT('Ctrl Pts',(16.2259135016087,-19.4649348073461,
18.5409440747148));
#149979=CARTESIAN_POINT('Ctrl Pts',(16.2086154222952,-19.3803527541242,
18.5452383772951));
#149980=CARTESIAN_POINT('Ctrl Pts',(16.1956204803925,-19.294991452669,18.5495326798753));
#149981=CARTESIAN_POINT('Ctrl Pts',(16.1869656326132,-19.2093245642189,
18.5538269824556));
#149982=CARTESIAN_POINT('Ctrl Pts',(16.1783107848339,-19.1236576757689,
18.5581212850358));
#149983=CARTESIAN_POINT('Ctrl Pts',(16.1739959871027,-19.0376857298059,
18.5624155876161));
#149984=CARTESIAN_POINT('Ctrl Pts',(16.1740000028035,-18.9518801919504,
18.5667098901964));
#149985=CARTESIAN_POINT('Ctrl Pts',(16.1740000028035,-18.9518801913083,
18.5667098902285));
#149986=CARTESIAN_POINT('Ctrl Pts',(16.1740003013853,-18.945500276023,18.5670291853155));
#149987=CARTESIAN_POINT('Ctrl Pts',(16.1740244495167,-18.9391204260769,
18.5673484804024));
#149988=CARTESIAN_POINT('Ctrl Pts',(16.1740724460423,-18.9327407557765,
18.5676677754894));
#149989=CARTESIAN_POINT('Ctrl Pts',(16.1747014814392,-18.8491297362399,
18.5718524098819));
#149990=CARTESIAN_POINT('Ctrl Pts',(16.1794322843349,-18.7653939703416,
18.5760370442745));
#149991=CARTESIAN_POINT('Ctrl Pts',(16.1882813814472,-18.6819690477863,
18.580221678667));
#149992=CARTESIAN_POINT('Ctrl Pts',(16.1971178829649,-18.5986628702823,
18.5844003567505));
#149993=CARTESIAN_POINT('Ctrl Pts',(16.2100609870472,-18.515667110836,18.5885790348339));
#149994=CARTESIAN_POINT('Ctrl Pts',(16.2270752140172,-18.433417202922,18.5927577129174));
#149995=CARTESIAN_POINT('Ctrl Pts',(16.2443944087803,-18.3496930245081,
18.5970112908029));
#149996=CARTESIAN_POINT('Ctrl Pts',(16.2659321081157,-18.2667421815311,
18.6012648686885));
#149997=CARTESIAN_POINT('Ctrl Pts',(16.2915956147072,-18.1850183713396,
18.605518446574));
#149998=CARTESIAN_POINT('Ctrl Pts',(16.3167615841415,-18.1048789366913,
18.6096895605515));
#149999=CARTESIAN_POINT('Ctrl Pts',(16.3458946705844,-18.0259198416596,
18.613860674529));
#150000=CARTESIAN_POINT('Ctrl Pts',(16.3788563531112,-17.9485567268056,
18.6180317885065));
#150001=CARTESIAN_POINT('Ctrl Pts',(16.411806975027,-17.8712195718919,18.6222015028263));
#150002=CARTESIAN_POINT('Ctrl Pts',(16.4485834613785,-17.79547775642,18.6263712171462));
#150003=CARTESIAN_POINT('Ctrl Pts',(16.4889988104968,-17.7217278109584,
18.6305409314661));
#150004=CARTESIAN_POINT('Ctrl Pts',(16.5294127214635,-17.6479804898363,
18.6347104974097));
#150005=CARTESIAN_POINT('Ctrl Pts',(16.5734650159172,-17.5762253008164,
18.6388800633533));
#150006=CARTESIAN_POINT('Ctrl Pts',(16.620922959331,-17.5068337741985,18.6430496292968));
#150007=CARTESIAN_POINT('Ctrl Pts',(16.6700494655017,-17.4350025270905,
18.6473657920363));
#150008=CARTESIAN_POINT('Ctrl Pts',(16.7228252639786,-17.3657046830183,
18.6516819547758));
#150009=CARTESIAN_POINT('Ctrl Pts',(16.7789448088305,-17.2993175745228,
18.6559981175153));
#150010=CARTESIAN_POINT('Ctrl Pts',(16.8332362653982,-17.2350930191197,
18.6601736817066));
#150011=CARTESIAN_POINT('Ctrl Pts',(16.8906566126944,-17.1735927891267,
18.6643492458978));
#150012=CARTESIAN_POINT('Ctrl Pts',(16.9508909514351,-17.1151216368725,
18.668524810089));
#150013=CARTESIAN_POINT('Ctrl Pts',(17.0141675834549,-17.0536972456977,
18.6729112721026));
#150014=CARTESIAN_POINT('Ctrl Pts',(17.0805495076473,-16.9956163559342,
18.6772977341163));
#150015=CARTESIAN_POINT('Ctrl Pts',(17.1496333442479,-16.9411836731961,
18.6816841961299));
#150016=CARTESIAN_POINT('Ctrl Pts',(17.2187171808487,-16.886750990458,18.6860706581436));
#150017=CARTESIAN_POINT('Ctrl Pts',(17.2905024122582,-16.835966787744,18.6904571201572));
#150018=CARTESIAN_POINT('Ctrl Pts',(17.3645537444778,-16.7890813808106,
18.6948435821709));
#150019=CARTESIAN_POINT('Ctrl Pts',(17.4351978651041,-16.7443532409684,
18.6990282165633));
#150020=CARTESIAN_POINT('Ctrl Pts',(17.5081670866298,-16.703006515634,18.7032128509558));
#150021=CARTESIAN_POINT('Ctrl Pts',(17.5831040926459,-16.665290877607,18.7073974853483));
#150022=CARTESIAN_POINT('Ctrl Pts',(17.6579344351092,-16.6276289231224,
18.7115761634316));
#150023=CARTESIAN_POINT('Ctrl Pts',(17.734726591191,-16.5935879949174,18.715754841515));
#150024=CARTESIAN_POINT('Ctrl Pts',(17.813095225772,-16.5633739520795,18.7199335195984));
#150025=CARTESIAN_POINT('Ctrl Pts',(17.8928685618193,-16.532618344233,18.7241870974839));
#150026=CARTESIAN_POINT('Ctrl Pts',(17.974275041662,-16.5058284229431,18.7284406753695));
#150027=CARTESIAN_POINT('Ctrl Pts',(18.0568830023301,-16.4831718222066,
18.7326942532551));
#150028=CARTESIAN_POINT('Ctrl Pts',(18.13788944647,-16.4609544638901,18.7368653672325));
#150029=CARTESIAN_POINT('Ctrl Pts',(18.2200507369796,-16.4427117186152,
18.7410364812098));
#150030=CARTESIAN_POINT('Ctrl Pts',(18.3029424071743,-16.428552090558,18.7452075951871));
#150031=CARTESIAN_POINT('Ctrl Pts',(18.3858062622686,-16.4143972139007,
18.7493773095069));
#150032=CARTESIAN_POINT('Ctrl Pts',(18.4693995572162,-16.4043228107592,
18.7535470238267));
#150033=CARTESIAN_POINT('Ctrl Pts',(18.5532876521047,-16.3983862767994,
18.7577167381465));
#150034=CARTESIAN_POINT('Ctrl Pts',(18.6371727618947,-16.3924499540871,
18.7618863040899));
#150035=CARTESIAN_POINT('Ctrl Pts',(18.7213521918228,-16.3906512394234,
18.7660558700333));
#150036=CARTESIAN_POINT('Ctrl Pts',(18.8053875689175,-16.3929955422071,
18.7702254359768));
#150037=CARTESIAN_POINT('Ctrl Pts',(18.892377526229,-16.3954222677854,18.7745415987164));
#150038=CARTESIAN_POINT('Ctrl Pts',(18.9792125852184,-16.4022887536939,
18.778857761456));
#150039=CARTESIAN_POINT('Ctrl Pts',(19.0654100827153,-16.413542327106,18.7831739241957));
#150040=CARTESIAN_POINT('Ctrl Pts',(19.1487997057718,-16.4244293165444,
18.7873494883867));
#150041=CARTESIAN_POINT('Ctrl Pts',(19.2315922114997,-16.4394218336012,
18.7915250525778));
#150042=CARTESIAN_POINT('Ctrl Pts',(19.3133609024087,-16.4584200544679,
18.7957006167689));
#150043=CARTESIAN_POINT('Ctrl Pts',(19.3992595355482,-16.4783778303156,
18.8000870787828));
#150044=CARTESIAN_POINT('Ctrl Pts',(19.4840276488778,-16.5027564393573,
18.8044735407967));
#150045=CARTESIAN_POINT('Ctrl Pts',(19.567190691381,-16.5313816344174,18.8088600028106));
#150046=CARTESIAN_POINT('Ctrl Pts',(19.6503537338843,-16.5600068294774,
18.8132464648245));
#150047=CARTESIAN_POINT('Ctrl Pts',(19.7319111958456,-16.5928783231054,
18.8176329268384));
#150048=CARTESIAN_POINT('Ctrl Pts',(19.8114169849416,-16.6297655931066,
18.8220193888523));
#150049=CARTESIAN_POINT('Ctrl Pts',(19.8872645948574,-16.6649556251499,
18.8262040232484));
#150050=CARTESIAN_POINT('Ctrl Pts',(19.961527503306,-16.7039309946397,18.8303886576445));
#150051=CARTESIAN_POINT('Ctrl Pts',(20.0338023663788,-16.7465263981729,
18.8345732920406));
#150052=CARTESIAN_POINT('Ctrl Pts',(20.10597435513,-16.7890611724216,18.8387519701276));
#150053=CARTESIAN_POINT('Ctrl Pts',(20.1761635263181,-16.8352055143118,
18.8429306482147));
#150054=CARTESIAN_POINT('Ctrl Pts',(20.2439882104361,-16.8847468456079,
18.8471093263017));
#150055=CARTESIAN_POINT('Ctrl Pts',(20.3130286032089,-16.9351761696166,
18.8513629041863));
#150056=CARTESIAN_POINT('Ctrl Pts',(20.3796184709323,-16.9891252600217,
18.855616482071));
#150057=CARTESIAN_POINT('Ctrl Pts',(20.4433832089661,-17.0463218936806,
18.8598700599557));
#150058=CARTESIAN_POINT('Ctrl Pts',(20.5059117431836,-17.1024096590374,
18.8640411739367));
#150059=CARTESIAN_POINT('Ctrl Pts',(20.5657233532606,-17.1616198500918,
18.8682122879177));
#150060=CARTESIAN_POINT('Ctrl Pts',(20.62249704859,-17.2236542887874,18.8723834018987));
#150061=CARTESIAN_POINT('Ctrl Pts',(20.6792516929575,-17.285667911228,18.8765531162222));
#150062=CARTESIAN_POINT('Ctrl Pts',(20.7329701367994,-17.3505035600743,
18.8807228305456));
#150063=CARTESIAN_POINT('Ctrl Pts',(20.7833688571022,-17.4178268391281,
18.884892544869));
#150064=CARTESIAN_POINT('Ctrl Pts',(20.833765784002,-17.4851477225305,18.8890621108161));
#150065=CARTESIAN_POINT('Ctrl Pts',(20.8808429472263,-17.5549556913558,
18.8932316767632));
#150066=CARTESIAN_POINT('Ctrl Pts',(20.9243585153512,-17.6268850713133,
18.8974012427103));
#150067=CARTESIAN_POINT('Ctrl Pts',(20.9694040370984,-17.7013433994185,
18.9017174054456));
#150068=CARTESIAN_POINT('Ctrl Pts',(21.010632579499,-17.7780746406022,18.9060335681809));
#150069=CARTESIAN_POINT('Ctrl Pts',(21.0478271756457,-17.8566444407211,
18.9103497309162));
#150070=CARTESIAN_POINT('Ctrl Pts',(21.0838101617912,-17.9326548379834,
18.9145252951108));
#150071=CARTESIAN_POINT('Ctrl Pts',(21.1160178406327,-18.0103853983034,
18.9187008593055));
#150072=CARTESIAN_POINT('Ctrl Pts',(21.1443031849367,-18.0894233038831,
18.9228764235001));
#150073=CARTESIAN_POINT('Ctrl Pts',(21.1740171546712,-18.1724532259881,
18.9272628855057));
#150074=CARTESIAN_POINT('Ctrl Pts',(21.1994019743872,-18.2569254729962,
18.9316493475113));
#150075=CARTESIAN_POINT('Ctrl Pts',(21.2203472929199,-18.3423467059141,
18.9360358095169));
#150076=CARTESIAN_POINT('Ctrl Pts',(21.2412926114527,-18.4277679388319,
18.9404222715225));
#150077=CARTESIAN_POINT('Ctrl Pts',(21.2577983946029,-18.514137573478,18.9448087335281));
#150078=CARTESIAN_POINT('Ctrl Pts',(21.2698170137415,-18.6009557395155,
18.9491951955337));
#150079=CARTESIAN_POINT('Ctrl Pts',(21.2812826384042,-18.6837792730856,
18.9533798299225));
#150080=CARTESIAN_POINT('Ctrl Pts',(21.2887076244828,-18.7673192548721,
18.9575644643113));
#150081=CARTESIAN_POINT('Ctrl Pts',(21.2920126435715,-18.851147060883,18.9617490987001));
#150082=CARTESIAN_POINT('Ctrl Pts',(21.2953129583745,-18.934855548388,18.9659277767799));
#150083=CARTESIAN_POINT('Ctrl Pts',(21.294504936491,-19.0188505906155,18.9701064548596));
#150084=CARTESIAN_POINT('Ctrl Pts',(21.2895607321101,-19.1026961993451,
18.9742851329393));
#150085=CARTESIAN_POINT('Ctrl Pts',(21.2845279064127,-19.1880446804597,
18.9785387108258));
#150086=CARTESIAN_POINT('Ctrl Pts',(21.2752090914542,-19.2732378406073,
18.9827922887123));
#150087=CARTESIAN_POINT('Ctrl Pts',(21.2616304174303,-19.3578133473421,
18.9870458665988));
#150088=CARTESIAN_POINT('Ctrl Pts',(21.2483149925156,-19.4407491927399,
18.9912169805726));
#150089=CARTESIAN_POINT('Ctrl Pts',(21.2309034822292,-19.5230906447102,
18.9953880945464));
#150090=CARTESIAN_POINT('Ctrl Pts',(21.2094728610011,-19.6044064028251,
18.9995592085202));
#150091=CARTESIAN_POINT('Ctrl Pts',(21.1880494310247,-19.6856948746526,
19.0037289228364));
#150092=CARTESIAN_POINT('Ctrl Pts',(21.1626096856898,-19.7659578917013,
19.0078986371526));
#150093=CARTESIAN_POINT('Ctrl Pts',(21.1332813336496,-19.8447760536666,
19.0120683514689));
#150094=CARTESIAN_POINT('Ctrl Pts',(21.1039540252378,-19.9235914109442,
19.0162379174088));
#150095=CARTESIAN_POINT('Ctrl Pts',(21.0707385464732,-20.0009615845084,
19.0204074833488));
#150096=CARTESIAN_POINT('Ctrl Pts',(21.0338114728018,-20.0764852998459,
19.0245770492887));
#150097=CARTESIAN_POINT('Ctrl Pts',(20.9955860886931,-20.1546643360123,
19.0288932120326));
#150098=CARTESIAN_POINT('Ctrl Pts',(20.9533834858384,-20.2308641813314,
19.0332093747765));
#150099=CARTESIAN_POINT('Ctrl Pts',(20.9074514472649,-20.3046672933068,
19.0375255375203));
#150100=CARTESIAN_POINT('Ctrl Pts',(20.8630156401099,-20.3760662765228,
19.041701101708));
#150101=CARTESIAN_POINT('Ctrl Pts',(20.815089945817,-20.4452219153955,19.0458766658958));
#150102=CARTESIAN_POINT('Ctrl Pts',(20.7639418957712,-20.5117871328463,
19.0500522300835));
#150103=CARTESIAN_POINT('Ctrl Pts',(20.7102104791443,-20.5817144014031,
19.0544386921054));
#150104=CARTESIAN_POINT('Ctrl Pts',(20.6529230087043,-20.6487822429891,
19.0588251541273));
#150105=CARTESIAN_POINT('Ctrl Pts',(20.5924345734849,-20.7126308346942,
19.0632116161493));
#150106=CARTESIAN_POINT('Ctrl Pts',(20.5319461382654,-20.7764794263994,
19.0675980781712));
#150107=CARTESIAN_POINT('Ctrl Pts',(20.4682572109593,-20.837108423261,19.0719845401932));
#150108=CARTESIAN_POINT('Ctrl Pts',(20.4017623229462,-20.8942072068039,
19.0763710022151));
#150109=CARTESIAN_POINT('Ctrl Pts',(20.3665290238934,-20.9244618410507,
19.0786952339391));
#150110=CARTESIAN_POINT('Ctrl Pts',(20.3304358504976,-20.9537886281019,
19.0810194656631));
#150111=CARTESIAN_POINT('Ctrl Pts',(20.2935357468249,-20.9821350335323,
19.0833436973871));
#150112=CARTESIAN_POINT('Origin',(18.734,-18.952,-1.76670989022851));
#150113=CARTESIAN_POINT('',(20.2935357468249,-20.9821350335323,19.9498236325831));
#150114=CARTESIAN_POINT('',(20.2935357468249,-20.9821350335323,19.8833624910577));
#150115=CARTESIAN_POINT('',(20.2935357468249,-20.9821350335323,-1.76670989022851));
#150116=CARTESIAN_POINT('',(16.1740009418753,-18.9498040034616,19.4332901097715));
#150117=CARTESIAN_POINT('Ctrl Pts',(16.1740009418753,-18.9498040034616,
19.4332901097715));
#150118=CARTESIAN_POINT('Ctrl Pts',(16.1741094126172,-18.8233534412475,
19.4395926510339));
#150119=CARTESIAN_POINT('Ctrl Pts',(16.1835900621658,-18.6972910723228,
19.4458951922963));
#150120=CARTESIAN_POINT('Ctrl Pts',(16.2022529884095,-18.572715055265,19.4521977335588));
#150121=CARTESIAN_POINT('Ctrl Pts',(16.2064836512073,-18.5444751579424,
19.4536264444963));
#150122=CARTESIAN_POINT('Ctrl Pts',(16.2111860003678,-18.5163115073012,
19.4550551554338));
#150123=CARTESIAN_POINT('Ctrl Pts',(16.2163575306343,-18.4882367021355,
19.4564838663713));
#150124=CARTESIAN_POINT('Ctrl Pts',(16.2315047248245,-18.4060067810516,
19.4606685004925));
#150125=CARTESIAN_POINT('Ctrl Pts',(16.25071296974,-18.3243667083971,19.4648531346137));
#150126=CARTESIAN_POINT('Ctrl Pts',(16.2739228554016,-18.2437483197165,
19.469037768735));
#150127=CARTESIAN_POINT('Ctrl Pts',(16.2970997046629,-18.1632446813365,
19.4732164465473));
#150128=CARTESIAN_POINT('Ctrl Pts',(16.3242667547544,-18.0837602766464,
19.4773951243597));
#150129=CARTESIAN_POINT('Ctrl Pts',(16.3553134075097,-18.0057177510347,
19.4815738021721));
#150130=CARTESIAN_POINT('Ctrl Pts',(16.3869165517615,-17.9262763628078,
19.4858273801254));
#150131=CARTESIAN_POINT('Ctrl Pts',(16.4225396637624,-17.8483295278622,
19.4900809580788));
#150132=CARTESIAN_POINT('Ctrl Pts',(16.4620126245779,-17.7723079359755,
19.4943345360321));
#150133=CARTESIAN_POINT('Ctrl Pts',(16.5007203219077,-17.6977601769908,
19.498505649741));
#150134=CARTESIAN_POINT('Ctrl Pts',(16.5431297041304,-17.6250641048156,
19.5026767634499));
#150135=CARTESIAN_POINT('Ctrl Pts',(16.5890321382659,-17.5546049691916,
19.5068478771588));
#150136=CARTESIAN_POINT('Ctrl Pts',(16.634919169412,-17.484169476787,19.5110175912116));
#150137=CARTESIAN_POINT('Ctrl Pts',(16.6842966737064,-17.4159698153114,
19.5151873052644));
#150138=CARTESIAN_POINT('Ctrl Pts',(16.7369115952916,-17.3503639914827,
19.5193570193173));
#150139=CARTESIAN_POINT('Ctrl Pts',(16.7895246446353,-17.2847605021618,
19.5235265849956));
#150140=CARTESIAN_POINT('Ctrl Pts',(16.8453745937438,-17.2217510253186,
19.527696150674));
#150141=CARTESIAN_POINT('Ctrl Pts',(16.9041676934287,-17.1616610014224,
19.5318657163523));
#150142=CARTESIAN_POINT('Ctrl Pts',(16.9650278943521,-17.0994582778473,
19.5361818794107));
#150143=CARTESIAN_POINT('Ctrl Pts',(17.0290416909462,-17.0403845007301,
19.540498042469));
#150144=CARTESIAN_POINT('Ctrl Pts',(17.0958426218327,-16.984758173392,19.5448142055274));
#150145=CARTESIAN_POINT('Ctrl Pts',(17.1604675106391,-16.9309438751296,
19.5489897694607));
#150146=CARTESIAN_POINT('Ctrl Pts',(17.2277003349621,-16.8803561190544,
19.5531653333939));
#150147=CARTESIAN_POINT('Ctrl Pts',(17.2971780335747,-16.8332403069725,
19.5573408973272));
#150148=CARTESIAN_POINT('Ctrl Pts',(17.370164900217,-16.7837447773015,19.5617273599481));
#150149=CARTESIAN_POINT('Ctrl Pts',(17.4456288796107,-16.7380814487272,
19.5661138225691));
#150150=CARTESIAN_POINT('Ctrl Pts',(17.523119783767,-16.696480303359,19.57050028519));
#150151=CARTESIAN_POINT('Ctrl Pts',(17.6006106879233,-16.6548791579908,
19.5748867478109));
#150152=CARTESIAN_POINT('Ctrl Pts',(17.6801279596806,-16.6173403747401,
19.5792732104318));
#150153=CARTESIAN_POINT('Ctrl Pts',(17.7611994326909,-16.5840348279075,
19.5836596730528));
#150154=CARTESIAN_POINT('Ctrl Pts',(17.8385406770861,-16.5522617227492,
19.587844307487));
#150155=CARTESIAN_POINT('Ctrl Pts',(17.9175841221718,-16.5242225928453,
19.5920289419213));
#150156=CARTESIAN_POINT('Ctrl Pts',(17.9979345050501,-16.5001012282021,
19.5962135763556));
#150157=CARTESIAN_POINT('Ctrl Pts',(18.078170519057,-16.4760141973499,19.6003922544782));
#150158=CARTESIAN_POINT('Ctrl Pts',(18.1597093389465,-16.4558339863015,
19.6045709326009));
#150159=CARTESIAN_POINT('Ctrl Pts',(18.2421357220942,-16.4396963694409,
19.6087496107236));
#150160=CARTESIAN_POINT('Ctrl Pts',(18.3260395379465,-16.4232694975869,
19.613003188599));
#150161=CARTESIAN_POINT('Ctrl Pts',(18.4108626031779,-16.411031755533,19.6172567664745));
#150162=CARTESIAN_POINT('Ctrl Pts',(18.4961506937665,-16.4030732243699,
19.6215103443499));
#150163=CARTESIAN_POINT('Ctrl Pts',(18.5797853091396,-16.3952689847841,
19.6256814583603));
#150164=CARTESIAN_POINT('Ctrl Pts',(18.6638666007976,-16.3915795598322,
19.6298525723707));
#150165=CARTESIAN_POINT('Ctrl Pts',(18.7479577055537,-16.3920380505844,
19.634023686381));
#150166=CARTESIAN_POINT('Ctrl Pts',(18.8320205926793,-16.3924963874854,
19.6381934007314));
#150167=CARTESIAN_POINT('Ctrl Pts',(18.9160928267199,-16.3970998732974,
19.6423631150818));
#150168=CARTESIAN_POINT('Ctrl Pts',(18.9997364062972,-16.4058295103493,
19.6465328294322));
#150169=CARTESIAN_POINT('Ctrl Pts',(19.0833770094284,-16.4145588367581,
19.6507023954039));
#150170=CARTESIAN_POINT('Ctrl Pts',(19.1665885309651,-16.4274139738732,
19.6548719613755));
#150171=CARTESIAN_POINT('Ctrl Pts',(19.2489383260598,-16.444324079879,19.6590415273471));
#150172=CARTESIAN_POINT('Ctrl Pts',(19.3341834370064,-16.461828724073,19.6633576900461));
#150173=CARTESIAN_POINT('Ctrl Pts',(19.4185045808358,-16.4836786817424,
19.667673852745));
#150174=CARTESIAN_POINT('Ctrl Pts',(19.5014355882166,-16.5097382167469,
19.6719900154439));
#150175=CARTESIAN_POINT('Ctrl Pts',(19.5816651279085,-16.5349488655021,
19.6761655796569));
#150176=CARTESIAN_POINT('Ctrl Pts',(19.6605932821671,-16.5640988419222,
19.68034114387));
#150177=CARTESIAN_POINT('Ctrl Pts',(19.7378171886914,-16.597015700331,19.684516708083));
#150178=CARTESIAN_POINT('Ctrl Pts',(19.81894148943,-16.6315951102716,19.6889031700249));
#150179=CARTESIAN_POINT('Ctrl Pts',(19.8981843303164,-16.6703316765417,
19.6932896319667));
#150180=CARTESIAN_POINT('Ctrl Pts',(19.9751086547792,-16.7129713474294,
19.6976760939086));
#150181=CARTESIAN_POINT('Ctrl Pts',(20.0520329792421,-16.7556110183172,
19.7020625558505));
#150182=CARTESIAN_POINT('Ctrl Pts',(20.1266383352645,-16.8021534221799,
19.7064490177923));
#150183=CARTESIAN_POINT('Ctrl Pts',(20.1985254700754,-16.8522940330845,
19.7108354797342));
#150184=CARTESIAN_POINT('Ctrl Pts',(20.2671049874831,-16.9001276114767,
19.7150201150503));
#150185=CARTESIAN_POINT('Ctrl Pts',(20.3334661901338,-16.9514136024954,
19.7192047503663));
#150186=CARTESIAN_POINT('Ctrl Pts',(20.3972405913418,-17.0059191344364,
19.7233893856824));
#150187=CARTESIAN_POINT('Ctrl Pts',(20.4609242176689,-17.0603470845722,
19.7275680646937));
#150188=CARTESIAN_POINT('Ctrl Pts',(20.5220280094205,-17.117985176789,19.7317467437049));
#150189=CARTESIAN_POINT('Ctrl Pts',(20.5802130388192,-17.1785577496591,
19.7359254227162));
#150190=CARTESIAN_POINT('Ctrl Pts',(20.6394409766887,-17.2402160253296,
19.7401790003703));
#150191=CARTESIAN_POINT('Ctrl Pts',(20.6956440915883,-17.304914740034,19.7444325780245));
#150192=CARTESIAN_POINT('Ctrl Pts',(20.7485007769389,-17.3723207225159,
19.7486861556786));
#150193=CARTESIAN_POINT('Ctrl Pts',(20.8003327466916,-17.4384199268452,
19.7528572705877));
#150194=CARTESIAN_POINT('Ctrl Pts',(20.8489465843956,-17.5071219871298,
19.7570283854968));
#150195=CARTESIAN_POINT('Ctrl Pts',(20.8940779914901,-17.5780774873814,
19.7611995004059));
#150196=CARTESIAN_POINT('Ctrl Pts',(20.9391942543019,-17.6490091778247,
19.7653692156568));
#150197=CARTESIAN_POINT('Ctrl Pts',(20.9808301606011,-17.7221924186382,
19.7695389309077));
#150198=CARTESIAN_POINT('Ctrl Pts',(21.0187646025466,-17.7972486367404,
19.7737086461586));
#150199=CARTESIAN_POINT('Ctrl Pts',(21.0566976946058,-17.8723021839882,
19.7778782130313));
#150200=CARTESIAN_POINT('Ctrl Pts',(21.0909293774472,-17.9492281650514,
19.7820477799041));
#150201=CARTESIAN_POINT('Ctrl Pts',(21.1212850353415,-18.0276244485954,
19.7862173467768));
#150202=CARTESIAN_POINT('Ctrl Pts',(21.1527079456952,-18.1087770099546,
19.7905335084134));
#150203=CARTESIAN_POINT('Ctrl Pts',(21.1799770112843,-18.1915046958175,
19.79484967005));
#150204=CARTESIAN_POINT('Ctrl Pts',(21.2029540362447,-18.275342060631,19.7991658316865));
#150205=CARTESIAN_POINT('Ctrl Pts',(21.2251825975804,-18.3564484705861,
19.8033413967929));
#150206=CARTESIAN_POINT('Ctrl Pts',(21.2433943908903,-18.438592905029,19.8075169618993));
#150207=CARTESIAN_POINT('Ctrl Pts',(21.2575163539161,-18.5213432787964,
19.8116925270058));
#150208=CARTESIAN_POINT('Ctrl Pts',(21.2723515733336,-18.6082731163458,
19.8160789869074));
#150209=CARTESIAN_POINT('Ctrl Pts',(21.2826728879139,-18.6958711330843,
19.8204654468091));
#150210=CARTESIAN_POINT('Ctrl Pts',(21.2884573444653,-18.7836323210737,
19.8248519067107));
#150211=CARTESIAN_POINT('Ctrl Pts',(21.2942418010168,-18.8713935090632,
19.8292383666124));
#150212=CARTESIAN_POINT('Ctrl Pts',(21.2954894673635,-18.959317287068,19.833624826514));
#150213=CARTESIAN_POINT('Ctrl Pts',(21.2922402934573,-19.0469031133929,
19.8380112864157));
#150214=CARTESIAN_POINT('Ctrl Pts',(21.2891403572398,-19.1304660383082,
19.8421962719868));
#150215=CARTESIAN_POINT('Ctrl Pts',(21.2819360687556,-19.214032439079,19.8463812575579));
#150216=CARTESIAN_POINT('Ctrl Pts',(21.2706237823411,-19.2971663176808,
19.8505662431291));
#150217=CARTESIAN_POINT('Ctrl Pts',(21.2593308428958,-19.380158015602,19.8547440712801));
#150218=CARTESIAN_POINT('Ctrl Pts',(21.2439439373072,-19.4627182103198,
19.8589218994311));
#150219=CARTESIAN_POINT('Ctrl Pts',(21.2245113674097,-19.5444129715016,
19.8630997275821));
#150220=CARTESIAN_POINT('Ctrl Pts',(21.2050977076966,-19.6260282340369,
19.8672734902131));
#150221=CARTESIAN_POINT('Ctrl Pts',(21.1816463054655,-19.7067792901258,
19.8714472528441));
#150222=CARTESIAN_POINT('Ctrl Pts',(21.1542568723985,-19.7862401762129,
19.8756210154751));
#150223=CARTESIAN_POINT('Ctrl Pts',(21.1268858754546,-19.8656475763201,
19.8797919687015));
#150224=CARTESIAN_POINT('Ctrl Pts',(21.0955822614975,-19.9437660975122,
19.8839629219279));
#150225=CARTESIAN_POINT('Ctrl Pts',(21.060495805953,-20.0201840969061,19.8881338751542));
#150226=CARTESIAN_POINT('Ctrl Pts',(21.0254224420283,-20.0965735828645,
19.8923032720953));
#150227=CARTESIAN_POINT('Ctrl Pts',(20.9865692332683,-20.1712633904095,
19.8964726690364));
#150228=CARTESIAN_POINT('Ctrl Pts',(20.9441338701724,-20.2438623285462,
19.9006420659775));
#150229=CARTESIAN_POINT('Ctrl Pts',(20.901681864461,-20.316489739073,19.9048130981037));
#150230=CARTESIAN_POINT('Ctrl Pts',(20.8556451222065,-20.3870242397313,
19.9089841302298));
#150231=CARTESIAN_POINT('Ctrl Pts',(20.8062666824532,-20.4551003947822,
19.9131551623559));
#150232=CARTESIAN_POINT('Ctrl Pts',(20.756880639097,-20.5231870326279,19.9173268367638));
#150233=CARTESIAN_POINT('Ctrl Pts',(20.7041521537777,-20.5888142054936,
19.9214985111717));
#150234=CARTESIAN_POINT('Ctrl Pts',(20.6483656430248,-20.651648253259,19.9256701855796));
#150235=CARTESIAN_POINT('Ctrl Pts',(20.592510493086,-20.7145596114319,19.9298469927755));
#150236=CARTESIAN_POINT('Ctrl Pts',(20.5335901158211,-20.7746706419221,
19.9340237999715));
#150237=CARTESIAN_POINT('Ctrl Pts',(20.4719267478643,-20.8316836486648,
19.9382006071674));
#150238=CARTESIAN_POINT('Ctrl Pts',(20.4147287607129,-20.8845680326222,
19.9420749489727));
#150239=CARTESIAN_POINT('Ctrl Pts',(20.3551712738705,-20.9347870462732,
19.9459492907779));
#150240=CARTESIAN_POINT('Ctrl Pts',(20.2935357468249,-20.9821350335323,
19.9498236325831));
#150241=CARTESIAN_POINT('Ctrl Pts',(20.2912840470176,-20.9792340293575,
19.149828721203));
#150242=CARTESIAN_POINT('Ctrl Pts',(20.0133685920828,-21.1947985603089,
19.1672632318048));
#150243=CARTESIAN_POINT('Ctrl Pts',(18.9167592873257,-21.7455418715826,
19.2270896779671));
#150244=CARTESIAN_POINT('Ctrl Pts',(16.8320816481898,-21.2027757351818,
19.3215765971073));
#150245=CARTESIAN_POINT('Ctrl Pts',(16.1790132429278,-19.6455867561426,
19.3986290056455));
#150246=CARTESIAN_POINT('Ctrl Pts',(16.1726852643248,-18.9498155443718,
19.4332894786233));
#150247=CARTESIAN_POINT('',(16.1740010149448,-18.9542795868247,19.3667098901939));
#150248=CARTESIAN_POINT('Ctrl Pts',(20.2935357468249,-20.9821350335323,
19.0833436973871));
#150249=CARTESIAN_POINT('Ctrl Pts',(20.2271546507136,-21.0331285342547,
19.0875248522918));
#150250=CARTESIAN_POINT('Ctrl Pts',(20.1581601935485,-21.0809470712519,
19.0917060071965));
#150251=CARTESIAN_POINT('Ctrl Pts',(20.0868893516481,-21.1253132314964,
19.0958871621012));
#150252=CARTESIAN_POINT('Ctrl Pts',(20.0157068422532,-21.1696244046804,
19.1000631349163));
#150253=CARTESIAN_POINT('Ctrl Pts',(19.9422539410436,-21.210491460075,19.1042391077314));
#150254=CARTESIAN_POINT('Ctrl Pts',(19.8668989098351,-21.2476785620148,
19.1084150805465));
#150255=CARTESIAN_POINT('Ctrl Pts',(19.7916121680322,-21.2848319636821,
19.1125872689467));
#150256=CARTESIAN_POINT('Ctrl Pts',(19.7144271328449,-21.3183118364559,
19.116759457347));
#150257=CARTESIAN_POINT('Ctrl Pts',(19.6357379828143,-21.3479275052368,
19.1209316457472));
#150258=CARTESIAN_POINT('Ctrl Pts',(19.5570861865498,-21.3775291154496,
19.1251018536082));
#150259=CARTESIAN_POINT('Ctrl Pts',(19.4769321230311,-21.4032700021637,
19.1292720614691));
#150260=CARTESIAN_POINT('Ctrl Pts',(19.3956902332643,-21.4250074878986,
19.1334422693301));
#150261=CARTESIAN_POINT('Ctrl Pts',(19.3144625382898,-21.4467411756041,
19.1376117485617));
#150262=CARTESIAN_POINT('Ctrl Pts',(19.232147839027,-21.4644727333422,19.1417812277932));
#150263=CARTESIAN_POINT('Ctrl Pts',(19.1491747117678,-21.4781096489877,
19.1459507070247));
#150264=CARTESIAN_POINT('Ctrl Pts',(19.0661911921266,-21.4917482726564,
19.1501207084834));
#150265=CARTESIAN_POINT('Ctrl Pts',(18.9825495348782,-21.5012911625872,
19.1542907099421));
#150266=CARTESIAN_POINT('Ctrl Pts',(18.898686097081,-21.506697338126,19.1584607114008));
#150267=CARTESIAN_POINT('Ctrl Pts',(18.8147324386056,-21.5121093296538,
19.1626351989665));
#150268=CARTESIAN_POINT('Ctrl Pts',(18.7305569831965,-21.5133756931289,
19.1668096865322));
#150269=CARTESIAN_POINT('Ctrl Pts',(18.6465982461443,-21.5105075597744,
19.170984174098));
#150270=CARTESIAN_POINT('Ctrl Pts',(18.56259038681,-21.5076377483426,19.1751611040582));
#150271=CARTESIAN_POINT('Ctrl Pts',(18.4787999566344,-21.5006286627532,
19.1793380340184));
#150272=CARTESIAN_POINT('Ctrl Pts',(18.3956600869716,-21.489543320468,19.1835149639786));
#150273=CARTESIAN_POINT('Ctrl Pts',(18.3123798101434,-21.478439257183,19.187698947966));
#150274=CARTESIAN_POINT('Ctrl Pts',(18.2297527398045,-21.4632452754277,
19.1918829319533));
#150275=CARTESIAN_POINT('Ctrl Pts',(18.1482012305168,-21.4440754004789,
19.1960669159406));
#150276=CARTESIAN_POINT('Ctrl Pts',(18.0996034855829,-21.4326517897902,
19.1985602135926));
#150277=CARTESIAN_POINT('Ctrl Pts',(18.0513874070201,-21.4198172442631,
19.2010535112446));
#150278=CARTESIAN_POINT('Ctrl Pts',(18.0036392138265,-21.4056041086573,
19.2035468088966));
#150279=CARTESIAN_POINT('Ctrl Pts',(17.9235008748327,-21.3817494451997,
19.2077314433107));
#150280=CARTESIAN_POINT('Ctrl Pts',(17.8443833236107,-21.3539201055369,
19.2119160777248));
#150281=CARTESIAN_POINT('Ctrl Pts',(17.7667095652025,-21.3222213429866,
19.2161007121389));
#150282=CARTESIAN_POINT('Ctrl Pts',(17.6891463657735,-21.2905676997005,
19.2202793902439));
#150283=CARTESIAN_POINT('Ctrl Pts',(17.6130232994484,-21.2550557457776,
19.224458068349));
#150284=CARTESIAN_POINT('Ctrl Pts',(17.5387487593335,-21.2158406462658,
19.228636746454));
#150285=CARTESIAN_POINT('Ctrl Pts',(17.4631429019428,-21.1759226445297,
19.2328903243342));
#150286=CARTESIAN_POINT('Ctrl Pts',(17.3894529543292,-21.1321675712374,
19.2371439022144));
#150287=CARTESIAN_POINT('Ctrl Pts',(17.3180889421044,-21.0847906311049,
19.2413974800945));
#150288=CARTESIAN_POINT('Ctrl Pts',(17.2481084600712,-21.0383321851128,
19.2455685940936));
#150289=CARTESIAN_POINT('Ctrl Pts',(17.1803649335769,-20.9883913190988,
19.2497397080926));
#150290=CARTESIAN_POINT('Ctrl Pts',(17.1152190899104,-20.9352166712514,
19.2539108220917));
#150291=CARTESIAN_POINT('Ctrl Pts',(17.0500951065615,-20.882059866671,19.2580805364331));
#150292=CARTESIAN_POINT('Ctrl Pts',(16.987567430963,-20.8256717259896,19.2622502507746));
#150293=CARTESIAN_POINT('Ctrl Pts',(16.9279649526829,-20.7663421418967,
19.266419965116));
#150294=CARTESIAN_POINT('Ctrl Pts',(16.8683645953157,-20.707014669006,19.270589531081));
#150295=CARTESIAN_POINT('Ctrl Pts',(16.8116895537435,-20.6447462859623,
19.2747590970461));
#150296=CARTESIAN_POINT('Ctrl Pts',(16.7582319859876,-20.5798638624914,
19.2789286630111));
#150297=CARTESIAN_POINT('Ctrl Pts',(16.7028949166956,-20.5127002537797,
19.283244825725));
#150298=CARTESIAN_POINT('Ctrl Pts',(16.6510061189315,-20.4427357723036,
19.2875609884389));
#150299=CARTESIAN_POINT('Ctrl Pts',(16.6028430768027,-20.370368840855,19.2918771511528));
#150300=CARTESIAN_POINT('Ctrl Pts',(16.5562489402055,-20.3003592538355,
19.2960527153651));
#150301=CARTESIAN_POINT('Ctrl Pts',(16.5131417547233,-20.2281017614849,
19.3002282795774));
#150302=CARTESIAN_POINT('Ctrl Pts',(16.4737266859787,-20.1539835880423,
19.3044038437897));
#150303=CARTESIAN_POINT('Ctrl Pts',(16.4323208564678,-20.0761218830912,
19.3087903057544));
#150304=CARTESIAN_POINT('Ctrl Pts',(16.3949901703475,-19.9962071202823,
19.3131767677191));
#150305=CARTESIAN_POINT('Ctrl Pts',(16.3619151438293,-19.9147115015028,
19.3175632296838));
#150306=CARTESIAN_POINT('Ctrl Pts',(16.3288401173112,-19.8332158827234,
19.3219496916486));
#150307=CARTESIAN_POINT('Ctrl Pts',(16.3000208686933,-19.7501399810729,
19.3263361536133));
#150308=CARTESIAN_POINT('Ctrl Pts',(16.2755767948947,-19.6659715292643,
19.330722615578));
#150309=CARTESIAN_POINT('Ctrl Pts',(16.2465257453528,-19.5659398453678,
19.3359357942364));
#150310=CARTESIAN_POINT('Ctrl Pts',(16.2235642356486,-19.464065347825,19.3411489728948));
#150311=CARTESIAN_POINT('Ctrl Pts',(16.2068848499427,-19.3610098022674,
19.3463621515532));
#150312=CARTESIAN_POINT('Ctrl Pts',(16.1904712789856,-19.2595966243872,
19.3514922492277));
#150313=CARTESIAN_POINT('Ctrl Pts',(16.1801412137013,-19.1570396545395,
19.3566223469021));
#150314=CARTESIAN_POINT('Ctrl Pts',(16.1760324691903,-19.0539907413612,
19.3617524445766));
#150315=CARTESIAN_POINT('Ctrl Pts',(16.1747089805837,-19.0207971314519,
19.363404926449));
#150316=CARTESIAN_POINT('Ctrl Pts',(16.1740306434087,-18.9875526505075,
19.3650574083215));
#150317=CARTESIAN_POINT('Ctrl Pts',(16.1740010149447,-18.9542795868247,
19.3667098901939));
#150318=CARTESIAN_POINT('Ctrl Pts',(16.1740010149441,-18.9542795861284,
19.3667098902285));
#150319=CARTESIAN_POINT('Ctrl Pts',(16.173926819566,-18.8709574030249,19.3708480242598));
#150320=CARTESIAN_POINT('Ctrl Pts',(16.1779248169782,-18.7875513930795,
19.374986158291));
#150321=CARTESIAN_POINT('Ctrl Pts',(16.1859928190662,-18.7044936245066,
19.3791242923222));
#150322=CARTESIAN_POINT('Ctrl Pts',(16.1940571655296,-18.6214734895413,
19.3832605513584));
#150323=CARTESIAN_POINT('Ctrl Pts',(16.2061878113244,-18.5388017480886,
19.3873968103945));
#150324=CARTESIAN_POINT('Ctrl Pts',(16.2223305526747,-18.456907496146,19.3915330694306));
#150325=CARTESIAN_POINT('Ctrl Pts',(16.238471016352,-18.3750247991377,19.3956687448579));
#150326=CARTESIAN_POINT('Ctrl Pts',(16.2586223602409,-18.2939198329686,
19.3998044202853));
#150327=CARTESIAN_POINT('Ctrl Pts',(16.2826791433887,-18.2140121559657,
19.4039400957127));
#150328=CARTESIAN_POINT('Ctrl Pts',(16.3067400382202,-18.1340908214803,
19.4080764779922));
#150329=CARTESIAN_POINT('Ctrl Pts',(16.3347075604887,-18.0553676300741,
19.4122128602717));
#150330=CARTESIAN_POINT('Ctrl Pts',(16.3664266589084,-17.9782461940757,
19.4163492425513));
#150331=CARTESIAN_POINT('Ctrl Pts',(16.3981808282496,-17.9010394870584,
19.4204901983132));
#150332=CARTESIAN_POINT('Ctrl Pts',(16.4336946710468,-17.8254385023485,
19.4246311540751));
#150333=CARTESIAN_POINT('Ctrl Pts',(16.4727655806441,-17.7518254707252,
19.4287721098371));
#150334=CARTESIAN_POINT('Ctrl Pts',(16.511861777281,-17.6781647960941,19.4329157456624));
#150335=CARTESIAN_POINT('Ctrl Pts',(16.5545193804023,-17.6064950352306,
19.4370593814876));
#150336=CARTESIAN_POINT('Ctrl Pts',(16.6004918491533,-17.5371703387789,
19.4412030173129));
#150337=CARTESIAN_POINT('Ctrl Pts',(16.6465392454185,-17.4677326545476,
19.4453534065787));
#150338=CARTESIAN_POINT('Ctrl Pts',(16.6959120078393,-17.4006480348314,
19.4495037958445));
#150339=CARTESIAN_POINT('Ctrl Pts',(16.7483230702929,-17.3362379102018,
19.4536541851102));
#150340=CARTESIAN_POINT('Ctrl Pts',(16.7661884610673,-17.3142823917967,
19.4550689308266));
#150341=CARTESIAN_POINT('Ctrl Pts',(16.7844065661398,-17.292637312599,19.4564836765431));
#150342=CARTESIAN_POINT('Ctrl Pts',(16.8029650799467,-17.2713143846827,
19.4578984222595));
#150343=CARTESIAN_POINT('Ctrl Pts',(16.857858757406,-17.2082439287342,19.4620830566462));
#150344=CARTESIAN_POINT('Ctrl Pts',(16.9159478005841,-17.1477482923964,
19.466267691033));
#150345=CARTESIAN_POINT('Ctrl Pts',(16.9769612646036,-17.0901689436695,
19.4704523254198));
#150346=CARTESIAN_POINT('Ctrl Pts',(17.0378878835037,-17.0326715520237,
19.4746310034971));
#150347=CARTESIAN_POINT('Ctrl Pts',(17.1017303233984,-16.9780825158866,
19.4788096815744));
#150348=CARTESIAN_POINT('Ctrl Pts',(17.1681782563647,-16.9267093376113,
19.4829883596517));
#150349=CARTESIAN_POINT('Ctrl Pts',(17.2358172209073,-16.8744153319337,
19.4872419375387));
#150350=CARTESIAN_POINT('Ctrl Pts',(17.306155687672,-16.8254539702902,19.4914955154258));
#150351=CARTESIAN_POINT('Ctrl Pts',(17.3788280009098,-16.780109382846,19.4957490933128));
#150352=CARTESIAN_POINT('Ctrl Pts',(17.4500914193922,-16.7356438888086,
19.4999202072833));
#150353=CARTESIAN_POINT('Ctrl Pts',(17.5235985912761,-16.6946564386902,
19.5040913212538));
#150354=CARTESIAN_POINT('Ctrl Pts',(17.5989738385239,-16.657372445741,19.5082624352243));
#150355=CARTESIAN_POINT('Ctrl Pts',(17.6743237928742,-16.6201009637983,
19.5124321495369));
#150356=CARTESIAN_POINT('Ctrl Pts',(17.7515401656506,-16.5865306747361,
19.5166018638495));
#150357=CARTESIAN_POINT('Ctrl Pts',(17.8302229081151,-16.556840930505,19.5207715781621));
#150358=CARTESIAN_POINT('Ctrl Pts',(17.9089028507046,-16.5271522427644,
19.5249411440981));
#150359=CARTESIAN_POINT('Ctrl Pts',(17.9890486285237,-16.5013439869149,
19.5291107100341));
#150360=CARTESIAN_POINT('Ctrl Pts',(18.070241741943,-16.4795467699346,19.5332802759701));
#150361=CARTESIAN_POINT('Ctrl Pts',(18.1542895053982,-16.4569831896062,
19.5375964387176));
#150362=CARTESIAN_POINT('Ctrl Pts',(18.2394591140174,-16.4387180891091,
19.5419126014652));
#150363=CARTESIAN_POINT('Ctrl Pts',(18.3252730114505,-16.4248390932053,
19.5462287642128));
#150364=CARTESIAN_POINT('Ctrl Pts',(18.4082915298621,-16.4114122041881,
19.5504043283958));
#150365=CARTESIAN_POINT('Ctrl Pts',(18.4919125329018,-16.402090058559,19.5545798925788));
#150366=CARTESIAN_POINT('Ctrl Pts',(18.5756985998716,-16.3968990887408,
19.5587554567618));
#150367=CARTESIAN_POINT('Ctrl Pts',(18.6637165024315,-16.3914459353448,
19.5631419187917));
#150368=CARTESIAN_POINT('Ctrl Pts',(18.75191599805,-16.3905522627807,19.5675283808215));
#150369=CARTESIAN_POINT('Ctrl Pts',(18.8397925195445,-16.3941868827437,
19.5719148428514));
#150370=CARTESIAN_POINT('Ctrl Pts',(18.927669041039,-16.3978215027067,19.5763013048812));
#150371=CARTESIAN_POINT('Ctrl Pts',(19.0152220177589,-16.4059842855989,
19.580687766911));
#150372=CARTESIAN_POINT('Ctrl Pts',(19.1019580505821,-16.4185819782334,
19.5850742289409));
#150373=CARTESIAN_POINT('Ctrl Pts',(19.1847032324225,-16.4306000327129,
19.5892588634749));
#150374=CARTESIAN_POINT('Ctrl Pts',(19.2670129891878,-16.4466985853912,
19.5934434980089));
#150375=CARTESIAN_POINT('Ctrl Pts',(19.3484535429803,-16.4668346446325,
19.5976281325429));
#150376=CARTESIAN_POINT('Ctrl Pts',(19.4297781762392,-16.4869420426893,
19.6018068107684));
#150377=CARTESIAN_POINT('Ctrl Pts',(19.5102356212338,-16.5110754227039,
19.6059854889938));
#150378=CARTESIAN_POINT('Ctrl Pts',(19.5893993425081,-16.5391402931715,
19.6101641672193));
#150379=CARTESIAN_POINT('Ctrl Pts',(19.6699820131946,-16.5677082050677,
19.6144177450694));
#150380=CARTESIAN_POINT('Ctrl Pts',(19.7492236469542,-16.6003498680241,
19.6186713229195));
#150381=CARTESIAN_POINT('Ctrl Pts',(19.8266874127979,-16.6369116176886,
19.6229249007697));
#150382=CARTESIAN_POINT('Ctrl Pts',(19.9026493955953,-16.6727645480079,
19.6270960148894));
#150383=CARTESIAN_POINT('Ctrl Pts',(19.9769013948655,-16.7123867192901,
19.6312671290091));
#150384=CARTESIAN_POINT('Ctrl Pts',(20.0490505263221,-16.7555842576552,
19.6354382431289));
#150385=CARTESIAN_POINT('Ctrl Pts',(20.1211754474381,-16.7987673006675,
19.6396079575908));
#150386=CARTESIAN_POINT('Ctrl Pts',(20.1911985077801,-16.8455230919237,
19.6437776720528));
#150387=CARTESIAN_POINT('Ctrl Pts',(20.2587523619284,-16.8956123335339,
19.6479473865147));
#150388=CARTESIAN_POINT('Ctrl Pts',(20.3263038122145,-16.9456997927494,
19.6521169526));
#150389=CARTESIAN_POINT('Ctrl Pts',(20.3913858619795,-16.9991201917914,
19.6562865186852));
#150390=CARTESIAN_POINT('Ctrl Pts',(20.4536621654943,-17.0555923337617,
19.6604560847705));
#150391=CARTESIAN_POINT('Ctrl Pts',(20.5181280223232,-17.1140499623236,
19.6647722473415));
#150392=CARTESIAN_POINT('Ctrl Pts',(20.5795867716016,-17.1757775704163,
19.6690884099125));
#150393=CARTESIAN_POINT('Ctrl Pts',(20.637706242632,-17.2404210384081,19.6734045724834));
#150394=CARTESIAN_POINT('Ctrl Pts',(20.6939324820634,-17.3029587567415,
19.6775801368139));
#150395=CARTESIAN_POINT('Ctrl Pts',(20.747033395186,-17.3682248892184,19.6817557011444));
#150396=CARTESIAN_POINT('Ctrl Pts',(20.796749988967,-17.4358659416078,19.6859312654749));
#150397=CARTESIAN_POINT('Ctrl Pts',(20.848977644148,-17.506923375185,19.6903177271661));
#150398=CARTESIAN_POINT('Ctrl Pts',(20.8974697909667,-17.5806014598665,
19.6947041888574));
#150399=CARTESIAN_POINT('Ctrl Pts',(20.9419795412608,-17.6564590529923,
19.6990906505486));
#150400=CARTESIAN_POINT('Ctrl Pts',(20.9864892915549,-17.732316646118,19.7034771122398));
#150401=CARTESIAN_POINT('Ctrl Pts',(21.0270164454133,-17.8103531977127,
19.7078635739311));
#150402=CARTESIAN_POINT('Ctrl Pts',(21.0633723464495,-17.8901033611523,
19.7122500356223));
#150403=CARTESIAN_POINT('Ctrl Pts',(21.0980554588832,-17.9661841020042,
19.7164346697446));
#150404=CARTESIAN_POINT('Ctrl Pts',(21.1290718315276,-18.0441074153777,
19.7206193038669));
#150405=CARTESIAN_POINT('Ctrl Pts',(21.1562228177886,-18.1234852922341,
19.7248039379892));
#150406=CARTESIAN_POINT('Ctrl Pts',(21.1833351579802,-18.202750184505,19.7289826158026));
#150407=CARTESIAN_POINT('Ctrl Pts',(21.2065928926806,-18.2834650962591,
19.7331612936161));
#150408=CARTESIAN_POINT('Ctrl Pts',(21.225844598729,-18.3652202322973,19.7373399714295));
#150409=CARTESIAN_POINT('Ctrl Pts',(21.2454413793526,-18.4484407771037,
19.7415935493826));
#150410=CARTESIAN_POINT('Ctrl Pts',(21.2608869019324,-18.5327387665076,
19.7458471273357));
#150411=CARTESIAN_POINT('Ctrl Pts',(21.2720739254929,-18.6176637190892,
19.7501007052888));
#150412=CARTESIAN_POINT('Ctrl Pts',(21.2830440658926,-18.700942229072,19.7542718189987));
#150413=CARTESIAN_POINT('Ctrl Pts',(21.2899192902196,-18.7848231321656,
19.7584429327087));
#150414=CARTESIAN_POINT('Ctrl Pts',(21.2926499549078,-18.8688711346757,
19.7626140464186));
#150415=CARTESIAN_POINT('Ctrl Pts',(21.2953797032961,-18.9528909340954,
19.7667837604725));
#150416=CARTESIAN_POINT('Ctrl Pts',(21.2939676391625,-19.0370772621646,
19.7709534745263));
#150417=CARTESIAN_POINT('Ctrl Pts',(21.2884161370488,-19.1209917121783,
19.7751231885802));
#150418=CARTESIAN_POINT('Ctrl Pts',(21.2828648324788,-19.2049031761927,
19.7792927542596));
#150419=CARTESIAN_POINT('Ctrl Pts',(21.2731744140114,-19.2885423224137,
19.783462319939));
#150420=CARTESIAN_POINT('Ctrl Pts',(21.2593992661682,-19.371474130832,19.7876318856184));
#150421=CARTESIAN_POINT('Ctrl Pts',(21.245139799164,-19.4573217311045,19.7919480486755));
#150422=CARTESIAN_POINT('Ctrl Pts',(21.2265031054957,-19.5424108076164,
19.7962642117326));
#150423=CARTESIAN_POINT('Ctrl Pts',(21.2036071461082,-19.6262703789217,
19.8005803747897));
#150424=CARTESIAN_POINT('Ctrl Pts',(21.181457023188,-19.7073982225301,19.804755938724));
#150425=CARTESIAN_POINT('Ctrl Pts',(21.1553210566128,-19.7873750003199,
19.8089315026582));
#150426=CARTESIAN_POINT('Ctrl Pts',(21.1253562910768,-19.8657916004908,
19.8131070665925));
#150427=CARTESIAN_POINT('Ctrl Pts',(21.0938780701787,-19.9481688531774,
19.817493529211));
#150428=CARTESIAN_POINT('Ctrl Pts',(21.0581743348026,-20.0288236424594,
19.8218799918296));
#150429=CARTESIAN_POINT('Ctrl Pts',(21.0184823804606,-20.1073095919992,
19.8262664544481));
#150430=CARTESIAN_POINT('Ctrl Pts',(20.9787904261185,-20.1857955415389,
19.8306529170666));
#150431=CARTESIAN_POINT('Ctrl Pts',(20.9351106070456,-20.262112185551,19.8350393796852));
#150432=CARTESIAN_POINT('Ctrl Pts',(20.887732090269,-20.3358490103134,19.8394258423037));
#150433=CARTESIAN_POINT('Ctrl Pts',(20.8425432910186,-20.4061779019346,
19.8436095735004));
#150434=CARTESIAN_POINT('Ctrl Pts',(20.7938219698895,-20.474421896084,19.847793304697));
#150435=CARTESIAN_POINT('Ctrl Pts',(20.7417867108824,-20.5402041819628,
19.8519770358936));
#150436=CARTESIAN_POINT('Ctrl Pts',(20.689816339456,-20.6059044378207,19.8561555500086));
#150437=CARTESIAN_POINT('Ctrl Pts',(20.6345405135828,-20.6691487197569,
19.8603340641236));
#150438=CARTESIAN_POINT('Ctrl Pts',(20.5762218026503,-20.7295879246439,
19.8645125782385));
#150439=CARTESIAN_POINT('Ctrl Pts',(20.5179688787956,-20.7899589504061,
19.8686863787337));
#150440=CARTESIAN_POINT('Ctrl Pts',(20.456680209172,-20.8475308583584,19.8728601792288));
#150441=CARTESIAN_POINT('Ctrl Pts',(20.3926584428826,-20.9019877358215,
19.8770339797239));
#150442=CARTESIAN_POINT('Ctrl Pts',(20.3603008450493,-20.9295110898671,
19.8791434835019));
#150443=CARTESIAN_POINT('Ctrl Pts',(20.3272457158191,-20.9562392675845,
19.8812529872798));
#150444=CARTESIAN_POINT('Ctrl Pts',(20.2935357468249,-20.9821350335323,
19.8833624910577));
#150445=CARTESIAN_POINT('Origin',(18.734,-18.952,-1.76670989022851));
#150446=CARTESIAN_POINT('',(20.293535746825,-20.9821350335323,20.7499611453528));
#150447=CARTESIAN_POINT('',(20.2916962225612,-20.9797764771361,20.6832232103036));
#150448=CARTESIAN_POINT('',(20.2935357468249,-20.9821350335323,-1.76670989022851));
#150449=CARTESIAN_POINT('',(16.1740004726297,-18.9535555911146,20.2332901098006));
#150450=CARTESIAN_POINT('Ctrl Pts',(16.1740004726297,-18.9535555911146,
20.2332901098006));
#150451=CARTESIAN_POINT('Ctrl Pts',(16.173950276098,-18.8709483454626,20.2374173417138));
#150452=CARTESIAN_POINT('Ctrl Pts',(16.1779027082632,-18.7881812209217,
20.2415445736269));
#150453=CARTESIAN_POINT('Ctrl Pts',(16.1858778001745,-18.7056805838826,
20.24567180554));
#150454=CARTESIAN_POINT('Ctrl Pts',(16.1940130436929,-18.6215232123815,
20.2498819183568));
#150455=CARTESIAN_POINT('Ctrl Pts',(16.2063343518257,-18.5376436404924,
20.2540920311735));
#150456=CARTESIAN_POINT('Ctrl Pts',(16.2228070334153,-18.4544963471735,
20.2583021439902));
#150457=CARTESIAN_POINT('Ctrl Pts',(16.2389199317137,-18.3731650913156,
20.2624203028504));
#150458=CARTESIAN_POINT('Ctrl Pts',(16.2590046102178,-18.2925349422861,
20.2665384617107));
#150459=CARTESIAN_POINT('Ctrl Pts',(16.2829763019886,-18.2130258246822,
20.270656620571));
#150460=CARTESIAN_POINT('Ctrl Pts',(16.306937024594,-18.1335530895192,20.27477289501));
#150461=CARTESIAN_POINT('Ctrl Pts',(16.3347810947711,-18.0552008202622,
20.2788891694489));
#150462=CARTESIAN_POINT('Ctrl Pts',(16.3663732871523,-17.9783759716349,
20.2830054438879));
#150463=CARTESIAN_POINT('Ctrl Pts',(16.3979610860963,-17.9015618068228,
20.2871211458883));
#150464=CARTESIAN_POINT('Ctrl Pts',(16.4332957915605,-17.8262750781318,
20.2912368478886));
#150465=CARTESIAN_POINT('Ctrl Pts',(16.4721937794553,-17.7529034147721,
20.2953525498889));
#150466=CARTESIAN_POINT('Ctrl Pts',(16.5126461134818,-17.6765998526872,
20.2996327134933));
#150467=CARTESIAN_POINT('Ctrl Pts',(16.5569522564909,-17.6023681227906,
20.3039128770976));
#150468=CARTESIAN_POINT('Ctrl Pts',(16.6048536565105,-17.5306148136394,
20.308193040702));
#150469=CARTESIAN_POINT('Ctrl Pts',(16.6509736167644,-17.4615299901315,
20.3123140262104));
#150470=CARTESIAN_POINT('Ctrl Pts',(16.7004258077716,-17.3947428571309,
20.3164350117188));
#150471=CARTESIAN_POINT('Ctrl Pts',(16.752937145384,-17.3305839626854,20.3205559972272));
#150472=CARTESIAN_POINT('Ctrl Pts',(16.8054841274566,-17.2663815174707,
20.3246797800421));
#150473=CARTESIAN_POINT('Ctrl Pts',(16.8610940674614,-17.2048112072835,
20.3288035628569));
#150474=CARTESIAN_POINT('Ctrl Pts',(16.9194565997149,-17.1461671593191,
20.3329273456718));
#150475=CARTESIAN_POINT('Ctrl Pts',(16.9779086863938,-17.0874331249574,
20.3370574562278));
#150476=CARTESIAN_POINT('Ctrl Pts',(17.0391214358428,-17.0316346193019,
20.3411875667839));
#150477=CARTESIAN_POINT('Ctrl Pts',(17.1027516837168,-16.9790253598631,
20.34531767734));
#150478=CARTESIAN_POINT('Ctrl Pts',(17.1099251001079,-16.9730944050642,
20.3457832892737));
#150479=CARTESIAN_POINT('Ctrl Pts',(17.117129212341,-16.9672039375623,20.3462489012075));
#150480=CARTESIAN_POINT('Ctrl Pts',(17.1243635072392,-16.9613542853705,
20.3467145131413));
#150481=CARTESIAN_POINT('Ctrl Pts',(17.1893810782662,-16.9087810654215,
20.3508991582797));
#150482=CARTESIAN_POINT('Ctrl Pts',(17.2570980357154,-16.8592987213468,
20.3550838034181));
#150483=CARTESIAN_POINT('Ctrl Pts',(17.3271882231892,-16.8131964502025,
20.3592684485566));
#150484=CARTESIAN_POINT('Ctrl Pts',(17.3971786444276,-16.7671598009406,
20.3634471372793));
#150485=CARTESIAN_POINT('Ctrl Pts',(17.4695352047632,-16.7244939187135,
20.367625826002));
#150486=CARTESIAN_POINT('Ctrl Pts',(17.5438988654958,-16.6854477085997,
20.3718045147248));
#150487=CARTESIAN_POINT('Ctrl Pts',(17.6195952011134,-16.6457017494008,
20.3760580899372));
#150488=CARTESIAN_POINT('Ctrl Pts',(17.6973709112956,-16.6097067832357,
20.3803116651496));
#150489=CARTESIAN_POINT('Ctrl Pts',(17.7768165359456,-16.5776790831607,
20.384565240362));
#150490=CARTESIAN_POINT('Ctrl Pts',(17.8547221935641,-16.5462722052193,
20.388736364645));
#150491=CARTESIAN_POINT('Ctrl Pts',(17.9342331580126,-16.5186803432953,
20.392907488928));
#150492=CARTESIAN_POINT('Ctrl Pts',(18.0149402978771,-16.4950602073346,
20.3970786132109));
#150493=CARTESIAN_POINT('Ctrl Pts',(18.0956203529298,-16.4714479981438,
20.4012483376907));
#150494=CARTESIAN_POINT('Ctrl Pts',(18.1774953450108,-16.4518049968894,
20.4054180621704));
#150495=CARTESIAN_POINT('Ctrl Pts',(18.2601401459595,-16.4362383183758,
20.4095877866501));
#150496=CARTESIAN_POINT('Ctrl Pts',(18.3427820029266,-16.42067219438,20.4137573625955));
#150497=CARTESIAN_POINT('Ctrl Pts',(18.4261931620004,-16.4091821887308,
20.4179269385409));
#150498=CARTESIAN_POINT('Ctrl Pts',(18.5099387943011,-16.401824206824,20.4220965144863));
#150499=CARTESIAN_POINT('Ctrl Pts',(18.5966283648553,-16.3942075673155,
20.426412664931));
#150500=CARTESIAN_POINT('Ctrl Pts',(18.6836758372579,-16.3910189213194,
20.4307288153757));
#150501=CARTESIAN_POINT('Ctrl Pts',(18.7705956997935,-16.3922615847012,
20.4350449658204));
#150502=CARTESIAN_POINT('Ctrl Pts',(18.8546845879848,-16.3934637746163,
20.4392205395221));
#150503=CARTESIAN_POINT('Ctrl Pts',(18.9386535841082,-16.3988129731103,
20.4433961132238));
#150504=CARTESIAN_POINT('Ctrl Pts',(19.022067326425,-16.4082592082827,20.4475716869256));
#150505=CARTESIAN_POINT('Ctrl Pts',(19.1096934356114,-16.4181824752605,
20.4519581257418));
#150506=CARTESIAN_POINT('Ctrl Pts',(19.1967061584434,-16.432627374484,20.456344564558));
#150507=CARTESIAN_POINT('Ctrl Pts',(19.28261403032,-16.4514755258674,20.4607310033742));
#150508=CARTESIAN_POINT('Ctrl Pts',(19.3685219021965,-16.4703236772508,
20.4651174421904));
#150509=CARTESIAN_POINT('Ctrl Pts',(19.4533243836861,-16.4935748540295,
20.4695038810066));
#150510=CARTESIAN_POINT('Ctrl Pts',(19.5365517912807,-16.5210514973961,
20.4738903198228));
#150511=CARTESIAN_POINT('Ctrl Pts',(19.6159508694346,-16.547264258518,20.478074989374));
#150512=CARTESIAN_POINT('Ctrl Pts',(19.6942121039237,-16.5774198563297,
20.4822596589251));
#150513=CARTESIAN_POINT('Ctrl Pts',(19.7709157801343,-16.6114005757267,
20.4864443284763));
#150514=CARTESIAN_POINT('Ctrl Pts',(19.847510283723,-16.645332930242,20.4906230419721));
#150515=CARTESIAN_POINT('Ctrl Pts',(19.9225512154519,-16.683079407488,20.4948017554679));
#150516=CARTESIAN_POINT('Ctrl Pts',(19.995634941963,-16.7244728344602,20.4989804689636));
#150517=CARTESIAN_POINT('Ctrl Pts',(20.070027857031,-16.7666077644113,20.5032340380278));
#150518=CARTESIAN_POINT('Ctrl Pts',(20.1423922959442,-16.8125214422593,
20.507487607092));
#150519=CARTESIAN_POINT('Ctrl Pts',(20.212324780906,-16.8619866406745,20.5117411761562));
#150520=CARTESIAN_POINT('Ctrl Pts',(20.280902218561,-16.9104933763104,20.5159123259083));
#150521=CARTESIAN_POINT('Ctrl Pts',(20.3471407144074,-16.9624149500114,
20.5200834756603));
#150522=CARTESIAN_POINT('Ctrl Pts',(20.4106870430868,-17.0174921660679,
20.5242546254124));
#150523=CARTESIAN_POINT('Ctrl Pts',(20.4742120492289,-17.0725509013401,
20.5284243755636));
#150524=CARTESIAN_POINT('Ctrl Pts',(20.5350463349135,-17.1307628750204,
20.5325941257149));
#150525=CARTESIAN_POINT('Ctrl Pts',(20.5928697180021,-17.19182859599,20.5367638758661));
#150526=CARTESIAN_POINT('Ctrl Pts',(20.6506910436328,-17.2528921441335,
20.5409334776502));
#150527=CARTESIAN_POINT('Ctrl Pts',(20.7055013639975,-17.3168089030567,
20.5451030794344));
#150528=CARTESIAN_POINT('Ctrl Pts',(20.7570183053472,-17.3832435063943,
20.5492726812186));
#150529=CARTESIAN_POINT('Ctrl Pts',(20.8103455378025,-17.452012603364,20.553588801659));
#150530=CARTESIAN_POINT('Ctrl Pts',(20.8601432986902,-17.5234793777062,
20.5579049220995));
#150531=CARTESIAN_POINT('Ctrl Pts',(20.906146010203,-17.5972373970474,20.56222104254));
#150532=CARTESIAN_POINT('Ctrl Pts',(20.9506510026991,-17.6685940625427,
20.5663966422274));
#150533=CARTESIAN_POINT('Ctrl Pts',(20.9916040781895,-17.7420946349332,
20.5705722419149));
#150534=CARTESIAN_POINT('Ctrl Pts',(21.0288116000799,-17.8173459910005,
20.5747478416023));
#150535=CARTESIAN_POINT('Ctrl Pts',(21.0678973296718,-17.8963959788854,
20.5791342224193));
#150536=CARTESIAN_POINT('Ctrl Pts',(21.102849178176,-17.9773776221854,20.5835206032363));
#150537=CARTESIAN_POINT('Ctrl Pts',(21.133500670816,-18.0598136233087,20.5879069840533));
#150538=CARTESIAN_POINT('Ctrl Pts',(21.164152163456,-18.1422496244321,20.5922933648703));
#150539=CARTESIAN_POINT('Ctrl Pts',(21.190503198929,-18.2261394071235,20.5966797456872));
#150540=CARTESIAN_POINT('Ctrl Pts',(21.2124488472332,-18.310991956643,20.6010661265042));
#150541=CARTESIAN_POINT('Ctrl Pts',(21.2333845648802,-18.3919396230659,
20.6052506476905));
#150542=CARTESIAN_POINT('Ctrl Pts',(21.2503893834069,-18.4740647142243,
20.6094351688768));
#150543=CARTESIAN_POINT('Ctrl Pts',(21.26333508953,-18.556950629829,20.6136196900631));
#150544=CARTESIAN_POINT('Ctrl Pts',(21.2762623681317,-18.6397185617595,
20.617798254807));
#150545=CARTESIAN_POINT('Ctrl Pts',(21.2851419407115,-18.723244716315,20.6219768195509));
#150546=CARTESIAN_POINT('Ctrl Pts',(21.2898958840996,-18.807099242091,20.6261553842948));
#150547=CARTESIAN_POINT('Ctrl Pts',(21.2947352019821,-18.892459683515,20.6304089904986));
#150548=CARTESIAN_POINT('Ctrl Pts',(21.2952991221815,-18.9781599402376,
20.6346625967024));
#150549=CARTESIAN_POINT('Ctrl Pts',(21.291560298641,-19.0637377233313,20.6389162029062));
#150550=CARTESIAN_POINT('Ctrl Pts',(21.2878940830978,-19.1476535848683,
20.6430872040273));
#150551=CARTESIAN_POINT('Ctrl Pts',(21.2800907694638,-19.2314512062989,
20.6472582051485));
#150552=CARTESIAN_POINT('Ctrl Pts',(21.2681770980697,-19.3146933079325,
20.6514292062696));
#150553=CARTESIAN_POINT('Ctrl Pts',(21.2562674233253,-19.3979074845461,
20.6555988081554));
#150554=CARTESIAN_POINT('Ctrl Pts',(21.2402501944418,-19.4805660564329,
20.6597684100413));
#150555=CARTESIAN_POINT('Ctrl Pts',(21.2202039195678,-19.5622377162434,
20.6639380119271));
#150556=CARTESIAN_POINT('Ctrl Pts',(21.2001583553194,-19.6439064808536,
20.6681074660036));
#150557=CARTESIAN_POINT('Ctrl Pts',(21.176084139551,-19.7245879563522,20.6722769200801));
#150558=CARTESIAN_POINT('Ctrl Pts',(21.1481104108277,-19.8038632075242,
20.6764463741566));
#150559=CARTESIAN_POINT('Ctrl Pts',(21.1191514853751,-19.8859304253638,
20.6807626707424));
#150560=CARTESIAN_POINT('Ctrl Pts',(21.0860134227954,-19.9664900212755,
20.6850789673281));
#150561=CARTESIAN_POINT('Ctrl Pts',(21.0488942544677,-20.045098618896,20.6893952639139));
#150562=CARTESIAN_POINT('Ctrl Pts',(21.0129862928853,-20.1211422004356,
20.6935707187789));
#150563=CARTESIAN_POINT('Ctrl Pts',(20.9733533017232,-20.1953597550482,
20.697746173644));
#150564=CARTESIAN_POINT('Ctrl Pts',(20.930221018763,-20.2673757017459,20.701921628509));
#150565=CARTESIAN_POINT('Ctrl Pts',(20.8849064017289,-20.3430353891307,
20.7063083459551));
#150566=CARTESIAN_POINT('Ctrl Pts',(20.8357293771905,-20.4162643215318,
20.7106950634012));
#150567=CARTESIAN_POINT('Ctrl Pts',(20.7830012667822,-20.4866640703179,
20.7150817808473));
#150568=CARTESIAN_POINT('Ctrl Pts',(20.730273156374,-20.557063819104,20.7194684982935));
#150569=CARTESIAN_POINT('Ctrl Pts',(20.6739943901059,-20.624633986963,20.7238552157396));
#150570=CARTESIAN_POINT('Ctrl Pts',(20.6145211534102,-20.689020492561,20.7282419331857));
#150571=CARTESIAN_POINT('Ctrl Pts',(20.5577980726924,-20.7504296432493,
20.7324258004444));
#150572=CARTESIAN_POINT('Ctrl Pts',(20.4979583003737,-20.8091716397172,
20.7366096677032));
#150573=CARTESIAN_POINT('Ctrl Pts',(20.4352825899291,-20.8649133668842,
20.7407935349619));
#150574=CARTESIAN_POINT('Ctrl Pts',(20.3895046482308,-20.905626771141,20.7438494050922));
#150575=CARTESIAN_POINT('Ctrl Pts',(20.3422147320298,-20.9447401724555,
20.7469052752225));
#150576=CARTESIAN_POINT('Ctrl Pts',(20.293535746825,-20.9821350335323,20.7499611453528));
#150577=CARTESIAN_POINT('Ctrl Pts',(20.2935357468249,-20.9821350335323,
19.9498236325831));
#150578=CARTESIAN_POINT('Ctrl Pts',(20.2269624064254,-21.0332762149925,
19.9540083599342));
#150579=CARTESIAN_POINT('Ctrl Pts',(20.1579647892918,-21.0810672001043,
19.9581930872852));
#150580=CARTESIAN_POINT('Ctrl Pts',(20.0869226462412,-21.1252925052297,
19.9623778146363));
#150581=CARTESIAN_POINT('Ctrl Pts',(20.0710253809767,-21.1351889044203,
19.9633142407899));
#150582=CARTESIAN_POINT('Ctrl Pts',(20.0550258276038,-21.1449069419241,
19.9642506669435));
#150583=CARTESIAN_POINT('Ctrl Pts',(20.0389283877474,-21.1544445288931,
19.965187093097));
#150584=CARTESIAN_POINT('Ctrl Pts',(19.9669932812531,-21.1970654264043,
19.9693717283983));
#150585=CARTESIAN_POINT('Ctrl Pts',(19.89283401806,-21.2362376726233,19.9735563636995));
#150586=CARTESIAN_POINT('Ctrl Pts',(19.8168151370648,-21.2717222633202,
19.9777409990007));
#150587=CARTESIAN_POINT('Ctrl Pts',(19.7409044598142,-21.3071563459651,
19.9819196779762));
#150588=CARTESIAN_POINT('Ctrl Pts',(19.6631398357117,-21.3389130062059,
19.9860983569518));
#150589=CARTESIAN_POINT('Ctrl Pts',(19.5839125153235,-21.3667978624093,
19.9902770359274));
#150590=CARTESIAN_POINT('Ctrl Pts',(19.5032651236308,-21.3951825270617,
19.9945306135879));
#150591=CARTESIAN_POINT('Ctrl Pts',(19.4211024978226,-21.419554974605,19.9987841912483));
#150592=CARTESIAN_POINT('Ctrl Pts',(19.3378610660991,-21.4397604010133,
20.0030377689088));
#150593=CARTESIAN_POINT('Ctrl Pts',(19.2562334111025,-21.4595741108662,
20.007208883732));
#150594=CARTESIAN_POINT('Ctrl Pts',(19.1735688735353,-21.4753808138571,
20.0113799985552));
#150595=CARTESIAN_POINT('Ctrl Pts',(19.0902949413618,-21.4870845971604,
20.0155511133785));
#150596=CARTESIAN_POINT('Ctrl Pts',(19.0070489529336,-21.4987844530938,
20.0197208285252));
#150597=CARTESIAN_POINT('Ctrl Pts',(18.9231944311978,-21.5063840596987,
20.0238905436719));
#150598=CARTESIAN_POINT('Ctrl Pts',(18.8391675225314,-21.509838890979,20.0280602588185));
#150599=CARTESIAN_POINT('Ctrl Pts',(18.7551436043038,-21.513293599305,20.032229825569));
#150600=CARTESIAN_POINT('Ctrl Pts',(18.670947771023,-21.5126038075443,20.0363993923194));
#150601=CARTESIAN_POINT('Ctrl Pts',(18.5870183641846,-21.5077770635822,
20.0405689590698));
#150602=CARTESIAN_POINT('Ctrl Pts',(18.5001381401371,-21.5027806193961,
20.0448851207956));
#150603=CARTESIAN_POINT('Ctrl Pts',(18.4135439525319,-21.4933509339464,
20.0492012825213));
#150604=CARTESIAN_POINT('Ctrl Pts',(18.3277166966688,-21.4795549207553,
20.053517444247));
#150605=CARTESIAN_POINT('Ctrl Pts',(18.2446852202507,-21.4662083057154,
20.0576930091878));
#150606=CARTESIAN_POINT('Ctrl Pts',(18.1623719289166,-21.4487756010914,
20.0618685741286));
#150607=CARTESIAN_POINT('Ctrl Pts',(18.0812003839157,-21.4273691969563,
20.0660441390694));
#150608=CARTESIAN_POINT('Ctrl Pts',(17.9959291092672,-21.4048816199831,
20.0704305991875));
#150609=CARTESIAN_POINT('Ctrl Pts',(17.9119185059158,-21.3780085540391,
20.0748170593057));
#150610=CARTESIAN_POINT('Ctrl Pts',(17.8296377675495,-21.3469381938825,
20.0792035194239));
#150611=CARTESIAN_POINT('Ctrl Pts',(17.7473570291832,-21.315867833726,20.0835899795421));
#150612=CARTESIAN_POINT('Ctrl Pts',(17.6668066567987,-21.2806004817434,
20.0879764396603));
#150613=CARTESIAN_POINT('Ctrl Pts',(17.5884257348681,-21.2413797419973,
20.0923628997785));
#150614=CARTESIAN_POINT('Ctrl Pts',(17.5136510990602,-21.2039635384314,
20.0965475399912));
#150615=CARTESIAN_POINT('Ctrl Pts',(17.4405723466444,-21.1628104733658,
20.100732180204));
#150616=CARTESIAN_POINT('Ctrl Pts',(17.3695877608619,-21.1180976990178,
20.1049168204167));
#150617=CARTESIAN_POINT('Ctrl Pts',(17.2987042121431,-21.0734485673238,
20.1090955043538));
#150618=CARTESIAN_POINT('Ctrl Pts',(17.2299092952355,-21.0252500336355,
20.1132741882909));
#150619=CARTESIAN_POINT('Ctrl Pts',(17.1635782312554,-20.9737258637741,
20.117452872228));
#150620=CARTESIAN_POINT('Ctrl Pts',(17.0960583483627,-20.9212782516533,
20.1217064486544));
#150621=CARTESIAN_POINT('Ctrl Pts',(17.0310919385808,-20.8653848344035,
20.1259600250807));
#150622=CARTESIAN_POINT('Ctrl Pts',(16.9690453966424,-20.8063287864041,
20.130213601507));
#150623=CARTESIAN_POINT('Ctrl Pts',(16.9082016411681,-20.748417553457,20.1343847213775));
#150624=CARTESIAN_POINT('Ctrl Pts',(16.8501659076099,-20.6874655440672,
20.138555841248));
#150625=CARTESIAN_POINT('Ctrl Pts',(16.7952502349276,-20.6237802931102,
20.1427269611185));
#150626=CARTESIAN_POINT('Ctrl Pts',(16.7403529896792,-20.5601164122958,
20.1468966813333));
#150627=CARTESIAN_POINT('Ctrl Pts',(16.6885740261885,-20.4937214595179,
20.151066401548));
#150628=CARTESIAN_POINT('Ctrl Pts',(16.6401868618211,-20.4249380646821,
20.1552361217628));
#150629=CARTESIAN_POINT('Ctrl Pts',(16.5918014193429,-20.3561571175489,
20.1594056935953));
#150630=CARTESIAN_POINT('Ctrl Pts',(16.5468077999962,-20.2849882740964,
20.1635752654278));
#150631=CARTESIAN_POINT('Ctrl Pts',(16.5054369234077,-20.2118041965518,
20.1677448372603));
#150632=CARTESIAN_POINT('Ctrl Pts',(16.4626116274946,-20.136047286488,20.1720609930269));
#150633=CARTESIAN_POINT('Ctrl Pts',(16.4236688015119,-20.0581312666225,
20.1763771487935));
#150634=CARTESIAN_POINT('Ctrl Pts',(16.3888124800457,-19.978496710297,20.1806933045602));
#150635=CARTESIAN_POINT('Ctrl Pts',(16.3550914981633,-19.9014560095544,
20.1848688745654));
#150636=CARTESIAN_POINT('Ctrl Pts',(16.3251950198264,-19.8228074630063,
20.1890444445707));
#150637=CARTESIAN_POINT('Ctrl Pts',(16.2992578088289,-19.7429680540524,
20.193220014576));
#150638=CARTESIAN_POINT('Ctrl Pts',(16.2720106919199,-19.6590965186773,
20.1976064632233));
#150639=CARTESIAN_POINT('Ctrl Pts',(16.2491334314107,-19.5739112339791,
20.2019929118706));
#150640=CARTESIAN_POINT('Ctrl Pts',(16.2307217504163,-19.4879085791077,
20.2063793605179));
#150641=CARTESIAN_POINT('Ctrl Pts',(16.2123100694219,-19.4019059242363,
20.2107658091652));
#150642=CARTESIAN_POINT('Ctrl Pts',(16.1983639848637,-19.3150864841139,
20.2151522578125));
#150643=CARTESIAN_POINT('Ctrl Pts',(16.1889163328206,-19.2279513128369,
20.2195387064599));
#150644=CARTESIAN_POINT('Ctrl Pts',(16.1790436177049,-19.1368958083959,
20.2241225075637));
#150645=CARTESIAN_POINT('Ctrl Pts',(16.1740562221029,-19.0453011470167,
20.2287063086676));
#150646=CARTESIAN_POINT('Ctrl Pts',(16.17400047263,-18.9535555916975,20.2332901097715));
#150647=CARTESIAN_POINT('',(16.1742339566945,-18.9509923323772,20.1667099326003));
#150648=CARTESIAN_POINT('Ctrl Pts',(20.2935357468249,-20.9821350335323,
19.8833624910577));
#150649=CARTESIAN_POINT('Ctrl Pts',(20.2268945255956,-21.0333283605784,
19.8875327680454));
#150650=CARTESIAN_POINT('Ctrl Pts',(20.1576922012557,-21.0812658913437,
19.891703045033));
#150651=CARTESIAN_POINT('Ctrl Pts',(20.0862835351796,-21.1256902356321,
19.8958733220206));
#150652=CARTESIAN_POINT('Ctrl Pts',(20.0148884140487,-21.1701061534178,
19.9000428079814));
#150653=CARTESIAN_POINT('Ctrl Pts',(19.9412881731929,-21.2110099658142,
19.9042122939422));
#150654=CARTESIAN_POINT('Ctrl Pts',(19.865865744466,-21.248188131775,19.9083817799029));
#150655=CARTESIAN_POINT('Ctrl Pts',(19.7904349973461,-21.2853703981421,
19.9125517257192));
#150656=CARTESIAN_POINT('Ctrl Pts',(19.7131820765029,-21.3188259999574,
19.9167216715355));
#150657=CARTESIAN_POINT('Ctrl Pts',(19.6345124063599,-21.3483884088336,
19.9208916173519));
#150658=CARTESIAN_POINT('Ctrl Pts',(19.5557587928649,-21.3779823618574,
19.9250660126495));
#150659=CARTESIAN_POINT('Ctrl Pts',(19.4755858434494,-21.4036746662349,
19.9292404079472));
#150660=CARTESIAN_POINT('Ctrl Pts',(19.3944162755987,-21.4253480027938,
19.9334148032449));
#150661=CARTESIAN_POINT('Ctrl Pts',(19.3132003061911,-21.4470337291756,
19.9375915848857));
#150662=CARTESIAN_POINT('Ctrl Pts',(19.2309870338681,-21.4646958169869,
19.9417683665265));
#150663=CARTESIAN_POINT('Ctrl Pts',(19.1482091842432,-21.478268147226,19.9459451481673));
#150664=CARTESIAN_POINT('Ctrl Pts',(19.0652902818818,-21.4918636045978,
19.9501290470077));
#150665=CARTESIAN_POINT('Ctrl Pts',(18.9818053382874,-21.5013553363726,
19.9543129458482));
#150666=CARTESIAN_POINT('Ctrl Pts',(18.898191710259,-21.5067291602599,19.9584968446886));
#150667=CARTESIAN_POINT('Ctrl Pts',(18.8442012325137,-21.5101991127764,
19.9611984461208));
#150668=CARTESIAN_POINT('Ctrl Pts',(18.7901571303858,-21.5119531845074,
19.963900047553));
#150669=CARTESIAN_POINT('Ctrl Pts',(18.7361763184532,-21.5119990749291,
19.9666016489852));
#150670=CARTESIAN_POINT('Ctrl Pts',(18.6525629441398,-21.5120701567241,
19.9707862842974));
#150671=CARTESIAN_POINT('Ctrl Pts',(18.5687904831801,-21.5080406575016,
19.9749709196097));
#150672=CARTESIAN_POINT('Ctrl Pts',(18.4852943717975,-21.4998904039421,
19.9791555549219));
#150673=CARTESIAN_POINT('Ctrl Pts',(18.401917106683,-21.4917517512489,19.9833342339293));
#150674=CARTESIAN_POINT('Ctrl Pts',(18.3188158637712,-21.479504039016,19.9875129129367));
#150675=CARTESIAN_POINT('Ctrl Pts',(18.2364263585064,-21.4631790998037,
19.9916915919441));
#150676=CARTESIAN_POINT('Ctrl Pts',(18.1525601036474,-21.4465615523608,
19.9959451695992));
#150677=CARTESIAN_POINT('Ctrl Pts',(18.0694318349346,-21.4257191735617,
20.0001987472543));
#150678=CARTESIAN_POINT('Ctrl Pts',(17.9874960097627,-21.4007408585965,
20.0044523249094));
#150679=CARTESIAN_POINT('Ctrl Pts',(17.9071486482337,-21.3762467902365,
20.0086234398147));
#150680=CARTESIAN_POINT('Ctrl Pts',(17.8279483680941,-21.3477758591386,
20.0127945547199));
#150681=CARTESIAN_POINT('Ctrl Pts',(17.7503119553381,-21.3154631012117,
20.0169656696251));
#150682=CARTESIAN_POINT('Ctrl Pts',(17.6727015942355,-21.283161186145,20.0211353848722));
#150683=CARTESIAN_POINT('Ctrl Pts',(17.5966544826745,-21.2470201811682,
20.0253051001192));
#150684=CARTESIAN_POINT('Ctrl Pts',(17.5225687032627,-21.2072237612453,
20.0294748153662));
#150685=CARTESIAN_POINT('Ctrl Pts',(17.4484855601723,-21.1674287574667,
20.0336443822352));
#150686=CARTESIAN_POINT('Ctrl Pts',(17.3763640153247,-21.1239788158135,
20.0378139491041));
#150687=CARTESIAN_POINT('Ctrl Pts',(17.306577534865,-21.0771035518365,20.041983515973));
#150688=CARTESIAN_POINT('Ctrl Pts',(17.2343374822408,-21.0285802345095,
20.0462996776141));
#150689=CARTESIAN_POINT('Ctrl Pts',(17.1646001862987,-20.9763865421866,
20.0506158392553));
#150690=CARTESIAN_POINT('Ctrl Pts',(17.0977455243704,-20.9208248502551,
20.0549320008964));
#150691=CARTESIAN_POINT('Ctrl Pts',(17.0330686154626,-20.8670730491965,
20.059107565999));
#150692=CARTESIAN_POINT('Ctrl Pts',(16.9710897386264,-20.8101696543991,
20.0632831311016));
#150693=CARTESIAN_POINT('Ctrl Pts',(16.9121162723824,-20.7504270024225,
20.0674586962043));
#150694=CARTESIAN_POINT('Ctrl Pts',(16.8501642397595,-20.6876669348877,
20.0718451561147));
#150695=CARTESIAN_POINT('Ctrl Pts',(16.7915295867437,-20.6217736911658,
20.0762316160251));
#150696=CARTESIAN_POINT('Ctrl Pts',(16.7365203854165,-20.5531480847578,
20.0806180759355));
#150697=CARTESIAN_POINT('Ctrl Pts',(16.6815111840894,-20.4845224783498,
20.0850045358459));
#150698=CARTESIAN_POINT('Ctrl Pts',(16.6301277117734,-20.4131650245491,
20.0893909957563));
#150699=CARTESIAN_POINT('Ctrl Pts',(16.5826239199876,-20.339508905323,20.0937774556667));
#150700=CARTESIAN_POINT('Ctrl Pts',(16.5362791661252,-20.2676499107529,
20.0980568909966));
#150701=CARTESIAN_POINT('Ctrl Pts',(16.4934601213991,-20.1933453656254,
20.1023363263266));
#150702=CARTESIAN_POINT('Ctrl Pts',(16.4544271376053,-20.1169667656347,
20.1066157616565));
#150703=CARTESIAN_POINT('Ctrl Pts',(16.4154575008855,-20.0407121213442,
20.1108882518421));
#150704=CARTESIAN_POINT('Ctrl Pts',(16.3802619051423,-19.9623904954392,
20.1151607420277));
#150705=CARTESIAN_POINT('Ctrl Pts',(16.3490570393213,-19.882401566158,20.1194332322133));
#150706=CARTESIAN_POINT('Ctrl Pts',(16.3179055660145,-19.8025495004692,
20.1236984120328));
#150707=CARTESIAN_POINT('Ctrl Pts',(16.2907313869642,-19.7210362103122,
20.1279635918524));
#150708=CARTESIAN_POINT('Ctrl Pts',(16.2677042874668,-19.6382838030585,
20.1322287716719));
#150709=CARTESIAN_POINT('Ctrl Pts',(16.2447004012897,-19.5556148174328,
20.136489651819));
#150710=CARTESIAN_POINT('Ctrl Pts',(16.2258353999309,-19.4717096122622,
20.1407505319661));
#150711=CARTESIAN_POINT('Ctrl Pts',(16.2112300227482,-19.3870076342743,
20.1450114121132));
#150712=CARTESIAN_POINT('Ctrl Pts',(16.1966372356338,-19.3023786707434,
20.1492686193135));
#150713=CARTESIAN_POINT('Ctrl Pts',(16.1862968405519,-19.2169547258213,
20.1535258265139));
#150714=CARTESIAN_POINT('Ctrl Pts',(16.1802787590759,-19.1311865610278,
20.1577830337143));
#150715=CARTESIAN_POINT('Ctrl Pts',(16.1760723590192,-19.0712380185088,
20.1607586525524));
#150716=CARTESIAN_POINT('Ctrl Pts',(16.1739765481552,-19.0111215762638,
20.1637342713904));
#150717=CARTESIAN_POINT('Ctrl Pts',(16.1740001980189,-18.950993095359,20.1667098902285));
#150718=CARTESIAN_POINT('Ctrl Pts',(16.1778405451444,-18.9509805605723,
20.166710586341));
#150719=CARTESIAN_POINT('Ctrl Pts',(16.17655678384,-18.5861666074448,20.1847914783433));
#150720=CARTESIAN_POINT('Ctrl Pts',(16.4202751438729,-17.3676607662538,
20.2452643059062));
#150721=CARTESIAN_POINT('Ctrl Pts',(18.2938122673756,-15.9570836117056,
20.3481290690295));
#150722=CARTESIAN_POINT('Ctrl Pts',(21.0139857521136,-16.9607793310482,
20.4753048757109));
#150723=CARTESIAN_POINT('Ctrl Pts',(21.565931935867,-19.4468145759116,20.5870029228023));
#150724=CARTESIAN_POINT('Ctrl Pts',(20.719740355667,-20.6463213593665,20.6563090343332));
#150725=CARTESIAN_POINT('Ctrl Pts',(20.2916962225613,-20.979776477136,20.6832232103036));
#150726=CARTESIAN_POINT('Origin',(18.734,-18.952,-1.76670989022851));
#150727=CARTESIAN_POINT('',(20.2910035915388,-20.9788220864065,21.5499225011608));
#150728=CARTESIAN_POINT('',(20.2957383325669,-20.9849679853861,21.4832513385096));
#150729=CARTESIAN_POINT('',(20.2935357468249,-20.9821350335323,-1.76670989022851));
#150730=CARTESIAN_POINT('',(16.1741052595683,-18.953341674122,21.0332900820446));
#150731=CARTESIAN_POINT('Ctrl Pts',(16.1775161375017,-18.9533393271451,
21.0332901097715));
#150732=CARTESIAN_POINT('Ctrl Pts',(16.179969922226,-18.4391275102653,21.0587831909243));
#150733=CARTESIAN_POINT('Ctrl Pts',(16.5801691895444,-17.06634175119,21.1266682076376));
#150734=CARTESIAN_POINT('Ctrl Pts',(18.8208064652996,-15.9262793346745,
21.2369451599114));
#150735=CARTESIAN_POINT('Ctrl Pts',(21.325440014071,-17.3869837941583,21.3641209665928));
#150736=CARTESIAN_POINT('Ctrl Pts',(21.4293000734299,-19.7637664899637,
21.4684467470093));
#150737=CARTESIAN_POINT('Ctrl Pts',(20.6042288430632,-20.7393377755163,
21.5303805918653));
#150738=CARTESIAN_POINT('Ctrl Pts',(20.2910035915388,-20.9788220864065,
21.5499225011608));
#150739=CARTESIAN_POINT('Ctrl Pts',(20.293535746825,-20.9821350335323,20.7499611453528));
#150740=CARTESIAN_POINT('Ctrl Pts',(20.223540407456,-21.0359049710261,20.7543551701242));
#150741=CARTESIAN_POINT('Ctrl Pts',(20.1506714756736,-21.0861194930542,
20.7587491948957));
#150742=CARTESIAN_POINT('Ctrl Pts',(20.075331422459,-21.1324655500888,20.7631432196671));
#150743=CARTESIAN_POINT('Ctrl Pts',(20.003802857654,-21.1764669384953,20.7673149486772));
#150744=CARTESIAN_POINT('Ctrl Pts',(19.9300475503307,-21.2169814550763,
20.7714866776873));
#150745=CARTESIAN_POINT('Ctrl Pts',(19.8544414350538,-21.2537843058407,
20.7756584066974));
#150746=CARTESIAN_POINT('Ctrl Pts',(19.7788660533636,-21.2905721963919,
20.7798284399162));
#150747=CARTESIAN_POINT('Ctrl Pts',(19.7014417708356,-21.3236512161474,
20.7839984731349));
#150748=CARTESIAN_POINT('Ctrl Pts',(19.6225688837902,-21.352842630986,20.7881685063537));
#150749=CARTESIAN_POINT('Ctrl Pts',(19.5437044012148,-21.3820309352706,
20.7923380952256));
#150750=CARTESIAN_POINT('Ctrl Pts',(19.4633920523903,-21.4073322986088,
20.7965076840975));
#150751=CARTESIAN_POINT('Ctrl Pts',(19.3820505778548,-21.4286167342853,
20.8006772729694));
#150752=CARTESIAN_POINT('Ctrl Pts',(19.3006933737931,-21.4499052858706,
20.8048476681416));
#150753=CARTESIAN_POINT('Ctrl Pts',(19.2183070941476,-21.4671752522082,
20.8090180633139));
#150754=CARTESIAN_POINT('Ctrl Pts',(19.1353227109471,-21.4803473024247,
20.8131884584861));
#150755=CARTESIAN_POINT('Ctrl Pts',(19.0522458578645,-21.4935340303177,
20.817363500749));
#150756=CARTESIAN_POINT('Ctrl Pts',(18.9685700262187,-21.5026136576386,
20.8215385430118));
#150757=CARTESIAN_POINT('Ctrl Pts',(18.884732829483,-21.5075585718422,20.8257135852747));
#150758=CARTESIAN_POINT('Ctrl Pts',(18.8008414639323,-21.5125066810493,
20.8298913251122));
#150759=CARTESIAN_POINT('Ctrl Pts',(18.7167889853071,-21.5133147558977,
20.8340690649496));
#150760=CARTESIAN_POINT('Ctrl Pts',(18.633012146745,-21.5100073208447,20.8382468047871));
#150761=CARTESIAN_POINT('Ctrl Pts',(18.5490995412421,-21.5066945258336,
20.8424313149797));
#150762=CARTESIAN_POINT('Ctrl Pts',(18.4654639244527,-21.4992529521216,
20.8466158251724));
#150763=CARTESIAN_POINT('Ctrl Pts',(18.3825355774442,-21.4877588133885,
20.8508003353651));
#150764=CARTESIAN_POINT('Ctrl Pts',(18.3520331048177,-21.4835310714315,
20.8523394701991));
#150765=CARTESIAN_POINT('Ctrl Pts',(18.3216262005314,-21.47875555542,20.8538786050331));
#150766=CARTESIAN_POINT('Ctrl Pts',(18.2913357986938,-21.4734377654192,
20.8554177398671));
#150767=CARTESIAN_POINT('Ctrl Pts',(18.208977638002,-21.458978947548,20.8596025742139));
#150768=CARTESIAN_POINT('Ctrl Pts',(18.1271754851468,-21.4404538825132,
20.8637874085606));
#150769=CARTESIAN_POINT('Ctrl Pts',(18.0463616913993,-21.4179184002202,
20.8679722429073));
#150770=CARTESIAN_POINT('Ctrl Pts',(17.9656628842856,-21.3954149827411,
20.8721511228248));
#150771=CARTESIAN_POINT('Ctrl Pts',(17.8859500822175,-21.3689126049628,
20.8763300027422));
#150772=CARTESIAN_POINT('Ctrl Pts',(17.8076468707951,-21.3385183594543,
20.8805088826597));
#150773=CARTESIAN_POINT('Ctrl Pts',(17.7279449213762,-21.3075811785374,
20.8847624103218));
#150774=CARTESIAN_POINT('Ctrl Pts',(17.6497038924681,-21.2726118027868,
20.8890159379838));
#150775=CARTESIAN_POINT('Ctrl Pts',(17.5733558319313,-21.2337767452422,
20.8932694656458));
#150776=CARTESIAN_POINT('Ctrl Pts',(17.4984833648361,-21.1956922602179,
20.8974407845723));
#150777=CARTESIAN_POINT('Ctrl Pts',(17.4254317742295,-21.1538904079626,
20.9016121034987));
#150778=CARTESIAN_POINT('Ctrl Pts',(17.3545880671759,-21.108576620383,20.9057834224251));
#150779=CARTESIAN_POINT('Ctrl Pts',(17.2837681192032,-21.0632780298334,
20.909953342403));
#150780=CARTESIAN_POINT('Ctrl Pts',(17.2151549713756,-21.0144700907621,
20.9141232623808));
#150781=CARTESIAN_POINT('Ctrl Pts',(17.149108758861,-20.9624028834442,20.9182931823587));
#150782=CARTESIAN_POINT('Ctrl Pts',(17.0830648895668,-20.9103375233926,
20.922462954394));
#150783=CARTESIAN_POINT('Ctrl Pts',(17.0195881352142,-20.8550134104489,
20.9266327264293));
#150784=CARTESIAN_POINT('Ctrl Pts',(16.9590064055076,-20.7967215886173,
20.9308024984647));
#150785=CARTESIAN_POINT('Ctrl Pts',(16.8963013133658,-20.7363866645938,
20.9351184191383));
#150786=CARTESIAN_POINT('Ctrl Pts',(16.8366983362714,-20.6728724968329,
20.939434339812));
#150787=CARTESIAN_POINT('Ctrl Pts',(16.7805189580978,-20.6065427824413,
20.9437502604856));
#150788=CARTESIAN_POINT('Ctrl Pts',(16.7261638999386,-20.542367001209,20.9479260297243));
#150789=CARTESIAN_POINT('Ctrl Pts',(16.6750137422496,-20.475556136878,20.952101798963));
#150790=CARTESIAN_POINT('Ctrl Pts',(16.6273169433956,-20.4064712094146,
20.9562775682017));
#150791=CARTESIAN_POINT('Ctrl Pts',(16.5772188714757,-20.3339082335378,
20.9606635645929));
#150792=CARTESIAN_POINT('Ctrl Pts',(16.5309313063379,-20.2588367080555,
20.965049560984));
#150793=CARTESIAN_POINT('Ctrl Pts',(16.488687917131,-20.1817047005368,20.9694355573751));
#150794=CARTESIAN_POINT('Ctrl Pts',(16.4464445279241,-20.1045726930181,
20.9738215537662));
#150795=CARTESIAN_POINT('Ctrl Pts',(16.408245498097,-20.0253807586022,20.9782075501574));
#150796=CARTESIAN_POINT('Ctrl Pts',(16.374265613089,-19.9445994273774,20.9825935465485));
#150797=CARTESIAN_POINT('Ctrl Pts',(16.3382155102257,-19.8588965093302,
20.9872467589128));
#150798=CARTESIAN_POINT('Ctrl Pts',(16.30679887472,-19.7711342279521,20.9918999712772));
#150799=CARTESIAN_POINT('Ctrl Pts',(16.2802296059439,-19.6818019274115,
20.9965531836415));
#150800=CARTESIAN_POINT('Ctrl Pts',(16.2537435506638,-19.5927494107485,
21.0011918223993));
#150801=CARTESIAN_POINT('Ctrl Pts',(16.2320746955043,-19.5021369352023,
21.0058304611572));
#150802=CARTESIAN_POINT('Ctrl Pts',(16.2153886011344,-19.4104720509521,
21.010469099915));
#150803=CARTESIAN_POINT('Ctrl Pts',(16.1987928068799,-19.3193032294376,
21.0150826357574));
#150804=CARTESIAN_POINT('Ctrl Pts',(16.1871261077823,-19.2270936177058,
21.0196961715999));
#150805=CARTESIAN_POINT('Ctrl Pts',(16.1805035115345,-19.1343614087313,
21.0243097074423));
#150806=CARTESIAN_POINT('Ctrl Pts',(16.1762064899349,-19.0741928147187,
21.0273031653588));
#150807=CARTESIAN_POINT('Ctrl Pts',(16.1740320413834,-19.0138045835855,
21.0302966232753));
#150808=CARTESIAN_POINT('Ctrl Pts',(16.1740003516178,-18.9533417463077,
21.0332900811918));
#150809=CARTESIAN_POINT('',(16.1715628046961,-18.9501455684938,20.9667098902285));
#150810=CARTESIAN_POINT('Ctrl Pts',(20.2916962225613,-20.979776477136,20.6832232103036));
#150811=CARTESIAN_POINT('Ctrl Pts',(20.0455373138351,-21.1715392921144,
20.6987009698937));
#150812=CARTESIAN_POINT('Ctrl Pts',(19.0022218507969,-21.7248575169448,
20.7565706650442));
#150813=CARTESIAN_POINT('Ctrl Pts',(16.8944629917136,-21.2791319918735,
20.8510662250192));
#150814=CARTESIAN_POINT('Ctrl Pts',(16.1775450733739,-19.6845343053476,
20.9300840254041));
#150815=CARTESIAN_POINT('Ctrl Pts',(16.1715628046961,-18.9501455684938,
20.9667098902285));
#150816=CARTESIAN_POINT('Ctrl Pts',(16.1715628046961,-18.9501455684938,
20.9667098902285));
#150817=CARTESIAN_POINT('Ctrl Pts',(16.1706210062014,-18.8345295298074,
20.9724759609646));
#150818=CARTESIAN_POINT('Ctrl Pts',(16.2303035994096,-17.8698877850362,
21.0206339672611));
#150819=CARTESIAN_POINT('Ctrl Pts',(17.4553333973082,-16.2082456258976,
21.1111839091181));
#150820=CARTESIAN_POINT('Ctrl Pts',(20.3489604080877,-16.3916498602743,
21.2383597157995));
#150821=CARTESIAN_POINT('Ctrl Pts',(21.7259567090655,-18.8613631150646,
21.3623821922634));
#150822=CARTESIAN_POINT('Ctrl Pts',(20.9160603918706,-20.5025267532674,
21.4440127331667));
#150823=CARTESIAN_POINT('Ctrl Pts',(20.2957383325669,-20.9849679853861,
21.4832513385096));
#150824=CARTESIAN_POINT('Origin',(-18.734,-18.952,-1.76670989022851));
#150825=CARTESIAN_POINT('',(-17.1724222076957,-20.9847558846529,0.749817803349287));
#150826=CARTESIAN_POINT('',(-17.1763092872519,-20.979697823649,0.683386607315289));
#150827=CARTESIAN_POINT('',(-17.1744641402401,-20.9821349467765,-1.76670989022851));
#150828=CARTESIAN_POINT('',(-21.2939992553243,-18.9500473764188,0.233290109771496));
#150829=CARTESIAN_POINT('Ctrl Pts',(-21.2960080607363,-18.9500458442149,
0.233290109771496));
#150830=CARTESIAN_POINT('Ctrl Pts',(-21.2971423972504,-18.8187089636245,
0.239839092339242));
#150831=CARTESIAN_POINT('Ctrl Pts',(-21.2281784586555,-17.8383740905167,
0.288780010467466));
#150832=CARTESIAN_POINT('Ctrl Pts',(-19.9618261937418,-16.1848209595297,
0.380112864156168));
#150833=CARTESIAN_POINT('Ctrl Pts',(-17.072091960026,-16.4220625707093,
0.507288670837601));
#150834=CARTESIAN_POINT('Ctrl Pts',(-15.7493320347114,-18.9005846102407,
0.630523650568644));
#150835=CARTESIAN_POINT('Ctrl Pts',(-16.5648621130939,-20.5111939119585,
0.711366694739205));
#150836=CARTESIAN_POINT('Ctrl Pts',(-17.1724222076957,-20.9847558846529,
0.749817803349287));
#150837=CARTESIAN_POINT('',(-18.0722323438033,-21.4249867709335,1.75387482315159E-11));
#150838=CARTESIAN_POINT('Ctrl Pts',(-18.0722323438033,-21.4249867709335,
1.75386372092134E-11));
#150839=CARTESIAN_POINT('Ctrl Pts',(-18.1529469590682,-21.4465858843588,
0.00418159276979397));
#150840=CARTESIAN_POINT('Ctrl Pts',(-18.2348713083479,-21.4642696834585,
0.00836318552204881));
#150841=CARTESIAN_POINT('Ctrl Pts',(-18.3175904330397,-21.4779063863382,
0.0125447782743042));
#150842=CARTESIAN_POINT('Ctrl Pts',(-18.4001917640921,-21.4915236702882,
0.0167204163572968));
#150843=CARTESIAN_POINT('Ctrl Pts',(-18.4835851718186,-21.5011052307699,
0.0208960544402894));
#150844=CARTESIAN_POINT('Ctrl Pts',(-18.5673419980694,-21.5065694569521,
0.0250716925232821));
#150845=CARTESIAN_POINT('Ctrl Pts',(-18.6514951828609,-21.5120595412382,
0.029267090784533));
#150846=CARTESIAN_POINT('Ctrl Pts',(-18.7360147805748,-21.5133930942776,
0.0334624890457846));
#150847=CARTESIAN_POINT('Ctrl Pts',(-18.8204570723939,-21.5105396566466,
0.0376578873070355));
#150848=CARTESIAN_POINT('Ctrl Pts',(-18.9043499961557,-21.5077047830247,
0.0418259909775979));
#150849=CARTESIAN_POINT('Ctrl Pts',(-18.988166150782,-21.5007372505448,
0.0459940946481601));
#150850=CARTESIAN_POINT('Ctrl Pts',(-19.0714685200797,-21.4896593541993,
0.0501621983187226));
#150851=CARTESIAN_POINT('Ctrl Pts',(-19.154742806599,-21.4785851924188,
0.0543288968439996));
#150852=CARTESIAN_POINT('Ctrl Pts',(-19.2375031954148,-21.4634034794687,
0.058495595369277));
#150853=CARTESIAN_POINT('Ctrl Pts',(-19.3193181247988,-21.4441883341317,
0.062662293894554));
#150854=CARTESIAN_POINT('Ctrl Pts',(-19.4011301114167,-21.424973879936,
0.0668288425496423));
#150855=CARTESIAN_POINT('Ctrl Pts',(-19.4819962578846,-21.4017263881227,
0.0709953912047298));
#150856=CARTESIAN_POINT('Ctrl Pts',(-19.5614968770273,-21.3745707251823,
0.0751619398598182));
#150857=CARTESIAN_POINT('Ctrl Pts',(-19.6419526867075,-21.347088790163,
0.0793785491042754));
#150858=CARTESIAN_POINT('Ctrl Pts',(-19.7210094734801,-21.3156042817862,
0.0835951583487334));
#150859=CARTESIAN_POINT('Ctrl Pts',(-19.7982514704291,-21.280297405335,
0.0878117675931906));
#150860=CARTESIAN_POINT('Ctrl Pts',(-19.8746836538426,-21.2453606900341,
0.0919841694456302));
#150861=CARTESIAN_POINT('Ctrl Pts',(-19.94933853646,-21.2066816487831,0.0961565712980696));
#150862=CARTESIAN_POINT('Ctrl Pts',(-20.0218382563897,-21.1644811016999,
0.100328973150509));
#150863=CARTESIAN_POINT('Ctrl Pts',(-20.0954901988233,-21.1216098703703,
0.104567686090975));
#150864=CARTESIAN_POINT('Ctrl Pts',(-20.1669174627927,-21.0751044941557,
0.108806399031441));
#150865=CARTESIAN_POINT('Ctrl Pts',(-20.2357562486613,-21.0252409820392,
0.113045111971908));
#150866=CARTESIAN_POINT('Ctrl Pts',(-20.3045950345299,-20.9753774699226,
0.117283824912374));
#150867=CARTESIAN_POINT('Ctrl Pts',(-20.3708449996543,-20.922156180229,
0.12152253785284));
#150868=CARTESIAN_POINT('Ctrl Pts',(-20.4341804646243,-20.8658929927532,
0.125761250793306));
#150869=CARTESIAN_POINT('Ctrl Pts',(-20.4958618762422,-20.8110991607781,
0.129889266554068));
#150870=CARTESIAN_POINT('Ctrl Pts',(-20.5550187782048,-20.7532072778741,
0.134017282314829));
#150871=CARTESIAN_POINT('Ctrl Pts',(-20.6113174681947,-20.6924824399031,
0.13814529807559));
#150872=CARTESIAN_POINT('Ctrl Pts',(-20.6675250873048,-20.6318558327154,
0.142266636202701));
#150873=CARTESIAN_POINT('Ctrl Pts',(-20.7208833621661,-20.5684057202645,
0.146387974329813));
#150874=CARTESIAN_POINT('Ctrl Pts',(-20.7710928145057,-20.5024363466744,
0.150509312456924));
#150875=CARTESIAN_POINT('Ctrl Pts',(-20.8212566402015,-20.4365269211813,
0.154626905416172));
#150876=CARTESIAN_POINT('Ctrl Pts',(-20.8682770342032,-20.3681031504801,
0.15874449837542));
#150877=CARTESIAN_POINT('Ctrl Pts',(-20.9118931740675,-20.2975041145794,
0.162862091334668));
#150878=CARTESIAN_POINT('Ctrl Pts',(-20.9554836015079,-20.2269466979588,
0.16697725690589));
#150879=CARTESIAN_POINT('Ctrl Pts',(-20.9956735091388,-20.1542169629418,
0.171092422477113));
#150880=CARTESIAN_POINT('Ctrl Pts',(-21.0322449112854,-20.0796836115467,
0.175207588048335));
#150881=CARTESIAN_POINT('Ctrl Pts',(-21.0688064249755,-20.0051704130512,
0.179321640929506));
#150882=CARTESIAN_POINT('Ctrl Pts',(-21.1017511684254,-19.928854991947,
0.183435693810676));
#150883=CARTESIAN_POINT('Ctrl Pts',(-21.1309074516109,-19.8511299507926,
0.187549746691847));
#150884=CARTESIAN_POINT('Ctrl Pts',(-21.1600799699192,-19.7733616299242,
0.191666090405279));
#150885=CARTESIAN_POINT('Ctrl Pts',(-21.1854596434762,-19.6941825637462,
0.195782434118711));
#150886=CARTESIAN_POINT('Ctrl Pts',(-21.2069235785594,-19.6140037572439,
0.199898777832143));
#150887=CARTESIAN_POINT('Ctrl Pts',(-21.2283934303839,-19.5338028486779,
0.204016256255544));
#150888=CARTESIAN_POINT('Ctrl Pts',(-21.2459452901289,-19.4526021135391,
0.208133734678947));
#150889=CARTESIAN_POINT('Ctrl Pts',(-21.25950720014,-19.3708238078728,0.212251213102348));
#150890=CARTESIAN_POINT('Ctrl Pts',(-21.2730871839159,-19.2889365174201,
0.216374178830764));
#150891=CARTESIAN_POINT('Ctrl Pts',(-21.2826665420701,-19.2064705900185,
0.22049714455918));
#150892=CARTESIAN_POINT('Ctrl Pts',(-21.2882251767647,-19.1238538518089,
0.224620110287596));
#150893=CARTESIAN_POINT('Ctrl Pts',(-21.2921215111921,-19.065943508881,
0.227510110115563));
#150894=CARTESIAN_POINT('Ctrl Pts',(-21.2940434271759,-19.0079591563185,
0.230400109943529));
#150895=CARTESIAN_POINT('Ctrl Pts',(-21.2939992553243,-18.9500473764188,
0.233290109771496));
#150896=CARTESIAN_POINT('',(-19.3957372685685,-21.4249949024184,0.));
#150897=CARTESIAN_POINT('Origin',(-18.734,-18.952,0.));
#150898=CARTESIAN_POINT('',(-21.2914666238416,-18.9551442278135,0.166709890228505));
#150899=CARTESIAN_POINT('Ctrl Pts',(-19.3957372685684,-21.4249949024184,
-8.32667268468867E-16));
#150900=CARTESIAN_POINT('Ctrl Pts',(-20.2191097516036,-21.2046724677036,
0.0423919355604773));
#150901=CARTESIAN_POINT('Ctrl Pts',(-21.1334435320312,-20.3367930039316,
0.0979618989699793));
#150902=CARTESIAN_POINT('Ctrl Pts',(-21.2935045362274,-19.2205935412502,
0.153531862379481));
#150903=CARTESIAN_POINT('Ctrl Pts',(-21.2914666238416,-18.9551442278135,
0.166709890228505));
#150904=CARTESIAN_POINT('Ctrl Pts',(-21.2914666238416,-18.9551442278135,
0.166709890228505));
#150905=CARTESIAN_POINT('Ctrl Pts',(-21.2869488473544,-18.3666789556461,
0.195923797939959));
#150906=CARTESIAN_POINT('Ctrl Pts',(-20.7940986851072,-16.9152596074165,
0.267529641211892));
#150907=CARTESIAN_POINT('Ctrl Pts',(-18.3819425606837,-15.9462796184213,
0.381527420044302));
#150908=CARTESIAN_POINT('Ctrl Pts',(-16.0159518620258,-17.6196571530585,
0.508703226725737));
#150909=CARTESIAN_POINT('Ctrl Pts',(-16.1161224269361,-19.9120072834025,
0.609322955816067));
#150910=CARTESIAN_POINT('Ctrl Pts',(-16.9218454647275,-20.7868241350996,
0.667550749345919));
#150911=CARTESIAN_POINT('Ctrl Pts',(-17.176309287252,-20.9796978236491,
0.683386607315295));
#150912=CARTESIAN_POINT('Origin',(-18.734,-18.952,-1.76670989022851));
#150913=CARTESIAN_POINT('',(-17.1739275047339,-20.9828452456382,1.55000082236256));
#150914=CARTESIAN_POINT('',(-17.1744641402401,-20.9821349467765,1.48324949998987));
#150915=CARTESIAN_POINT('',(-17.1744641402401,-20.9821349467765,-1.76670989022851));
#150916=CARTESIAN_POINT('',(-21.2964370736898,-18.9538544369521,1.0332901097715));
#150917=CARTESIAN_POINT('Ctrl Pts',(-21.2964370736898,-18.9538544369521,
1.0332901097715));
#150918=CARTESIAN_POINT('Ctrl Pts',(-21.2904548055299,-18.219465735772,
1.06991597459592));
#150919=CARTESIAN_POINT('Ctrl Pts',(-20.5735369171316,-16.6248681111266,
1.14893377498083));
#150920=CARTESIAN_POINT('Ctrl Pts',(-17.865447416609,-16.0521913171216,
1.27034351092621));
#150921=CARTESIAN_POINT('Ctrl Pts',(-15.8255862006271,-18.112700872363,
1.39751931760764));
#150922=CARTESIAN_POINT('Ctrl Pts',(-16.2862202722418,-20.1874548438184,
1.49073842141976));
#150923=CARTESIAN_POINT('Ctrl Pts',(-17.0385457522606,-20.8810080370261,
1.54156558967141));
#150924=CARTESIAN_POINT('Ctrl Pts',(-17.173927504734,-20.9828452456383,
1.55000082236257));
#150925=CARTESIAN_POINT('Ctrl Pts',(-17.1724222076957,-20.9847558846529,
0.749817803349287));
#150926=CARTESIAN_POINT('Ctrl Pts',(-17.2346906124658,-21.033290916597,
0.75375863029968));
#150927=CARTESIAN_POINT('Ctrl Pts',(-17.9939164669478,-21.567801595126,
0.800091392810553));
#150928=CARTESIAN_POINT('Ctrl Pts',(-20.0126665309401,-21.6957542121544,
0.888816090881905));
#150929=CARTESIAN_POINT('Ctrl Pts',(-21.2376962809792,-20.0341121664399,
0.979366032738912));
#150930=CARTESIAN_POINT('Ctrl Pts',(-21.2973788721029,-19.0694704700222,
1.02752403903544));
#150931=CARTESIAN_POINT('Ctrl Pts',(-21.2964370736898,-18.9538544369521,
1.0332901097715));
#150932=CARTESIAN_POINT('',(-21.2939288367578,-18.9506582997167,0.966709918232303));
#150933=CARTESIAN_POINT('Ctrl Pts',(-17.176309287252,-20.9796978236491,
0.683386607315295));
#150934=CARTESIAN_POINT('Ctrl Pts',(-17.6030345728764,-21.3031390068366,
0.709942684906398));
#150935=CARTESIAN_POINT('Ctrl Pts',(-18.9689508247891,-21.8140068744739,
0.778890698057982));
#150936=CARTESIAN_POINT('Ctrl Pts',(-20.8878308446456,-20.8376582577765,
0.873331792362382));
#150937=CARTESIAN_POINT('Ctrl Pts',(-21.2880301148004,-19.4648724899129,
0.941216809075682));
#150938=CARTESIAN_POINT('Ctrl Pts',(-21.2904838985449,-18.9506606701336,
0.966709890228504));
#150939=CARTESIAN_POINT('Ctrl Pts',(-21.2939996483808,-18.9506582509922,
0.966709918807928));
#150940=CARTESIAN_POINT('Ctrl Pts',(-21.2939507847444,-18.8574285254183,
0.971325634427595));
#150941=CARTESIAN_POINT('Ctrl Pts',(-21.2888049399727,-18.7643768813754,
0.975941350047264));
#150942=CARTESIAN_POINT('Ctrl Pts',(-21.2786450004472,-18.6720324631339,
0.980557065666932));
#150943=CARTESIAN_POINT('Ctrl Pts',(-21.2684492555577,-18.5793626073736,
0.98518904785764));
#150944=CARTESIAN_POINT('Ctrl Pts',(-21.2532041411694,-18.4874052362913,
0.989821030048348));
#150945=CARTESIAN_POINT('Ctrl Pts',(-21.2330434185021,-18.3966784783199,
0.994453012239056));
#150946=CARTESIAN_POINT('Ctrl Pts',(-21.2127838652416,-18.3055069654919,
0.999107701033865));
#150947=CARTESIAN_POINT('Ctrl Pts',(-21.1875605220101,-18.2155784195034,
1.00376238982867));
#150948=CARTESIAN_POINT('Ctrl Pts',(-21.1575575881288,-18.1273979038206,
1.00841707862348));
#150949=CARTESIAN_POINT('Ctrl Pts',(-21.1382431842027,-18.0706316520587,
1.01141353689948));
#150950=CARTESIAN_POINT('Ctrl Pts',(-21.1169490236919,-18.0145893782908,
1.01440999517548));
#150951=CARTESIAN_POINT('Ctrl Pts',(-21.0937343882856,-17.9594005758905,
1.01740645345148));
#150952=CARTESIAN_POINT('Ctrl Pts',(-21.0613129620801,-17.8823242120765,
1.02159128983477));
#150953=CARTESIAN_POINT('Ctrl Pts',(-21.0250509387666,-17.8066946664276,
1.02577612621805));
#150954=CARTESIAN_POINT('Ctrl Pts',(-20.9850989461096,-17.7329210301116,
1.02996096260134));
#150955=CARTESIAN_POINT('Ctrl Pts',(-20.9452038038475,-17.6592523712966,
1.03413984409765));
#150956=CARTESIAN_POINT('Ctrl Pts',(-20.9016293390032,-17.5874347771646,
1.03831872559397));
#150957=CARTESIAN_POINT('Ctrl Pts',(-20.8545742066751,-17.5178573871528,
1.04249760709029));
#150958=CARTESIAN_POINT('Ctrl Pts',(-20.8066785470568,-17.447037163635,
1.0467511343004));
#150959=CARTESIAN_POINT('Ctrl Pts',(-20.7551768351364,-17.3785384082051,
1.05100466151051));
#150960=CARTESIAN_POINT('Ctrl Pts',(-20.7003275395571,-17.3127452891087,
1.05525818872062));
#150961=CARTESIAN_POINT('Ctrl Pts',(-20.6465383152431,-17.2482237523413,
1.05942950809333));
#150962=CARTESIAN_POINT('Ctrl Pts',(-20.5895300617653,-17.1863045680918,
1.06360082746604));
#150963=CARTESIAN_POINT('Ctrl Pts',(-20.5295891698327,-17.1273193339164,
1.06777214683875));
#150964=CARTESIAN_POINT('Ctrl Pts',(-20.4696683865407,-17.0683538877827,
1.0719420668402));
#150965=CARTESIAN_POINT('Ctrl Pts',(-20.4068172462801,-17.0123207593134,
1.07611198684165));
#150966=CARTESIAN_POINT('Ctrl Pts',(-20.3413596900249,-16.9595154136398,
1.08028190684309));
#150967=CARTESIAN_POINT('Ctrl Pts',(-20.2759044627329,-16.9067119467669,
1.08445167847984));
#150968=CARTESIAN_POINT('Ctrl Pts',(-20.2078433623746,-16.8571363224976,
1.08862145011658));
#150969=CARTESIAN_POINT('Ctrl Pts',(-20.1375330967626,-16.8110434739837,
1.09279122175333));
#150970=CARTESIAN_POINT('Ctrl Pts',(-20.0647584945778,-16.763335096196,
1.0971071416183));
#150971=CARTESIAN_POINT('Ctrl Pts',(-19.9895745735351,-16.7193584596411,
1.10142306148326));
#150972=CARTESIAN_POINT('Ctrl Pts',(-19.912407443714,-16.6793460675678,
1.10573898134822));
#150973=CARTESIAN_POINT('Ctrl Pts',(-19.8377461836545,-16.640633009079,
1.10991474914186));
#150974=CARTESIAN_POINT('Ctrl Pts',(-19.7612289942279,-16.6056308240552,
1.11409051693549));
#150975=CARTESIAN_POINT('Ctrl Pts',(-19.6832631274217,-16.5745014164215,
1.11826628472913));
#150976=CARTESIAN_POINT('Ctrl Pts',(-19.6013720862765,-16.5418048056382,
1.12265228062976));
#150977=CARTESIAN_POINT('Ctrl Pts',(-19.5178832247939,-16.513381343314,
1.12703827653039));
#150978=CARTESIAN_POINT('Ctrl Pts',(-19.4332853705763,-16.4893591470744,
1.13142427243102));
#150979=CARTESIAN_POINT('Ctrl Pts',(-19.3486875163586,-16.4653369508349,
1.13581026833165));
#150980=CARTESIAN_POINT('Ctrl Pts',(-19.262981251447,-16.4457160760172,
1.14019626423228));
#150981=CARTESIAN_POINT('Ctrl Pts',(-19.1766642016327,-16.4305622346382,
1.14458226013291));
#150982=CARTESIAN_POINT('Ctrl Pts',(-19.094308163638,-16.4161037894172,
1.14876698662453));
#150983=CARTESIAN_POINT('Ctrl Pts',(-19.0110898349947,-16.4056576058547,
1.15295171311615));
#150984=CARTESIAN_POINT('Ctrl Pts',(-18.9274347085164,-16.3993184660947,
1.15713643960778));
#150985=CARTESIAN_POINT('Ctrl Pts',(-18.8438986079916,-16.3929883457718,
1.16131521199853));
#150986=CARTESIAN_POINT('Ctrl Pts',(-18.7599273988698,-16.3907536965201,
1.16549398438929));
#150987=CARTESIAN_POINT('Ctrl Pts',(-18.6759557948522,-16.3926581177481,
1.16967275678004));
#150988=CARTESIAN_POINT('Ctrl Pts',(-18.5904814574488,-16.3945966199894,
1.1739263113648));
#150989=CARTESIAN_POINT('Ctrl Pts',(-18.5050071857135,-16.4008238803847,
1.17817986594957));
#150990=CARTESIAN_POINT('Ctrl Pts',(-18.4199959336435,-16.4113305121855,
1.18243342053433));
#150991=CARTESIAN_POINT('Ctrl Pts',(-18.3366303540414,-16.4216337535614,
1.18660463357606));
#150992=CARTESIAN_POINT('Ctrl Pts',(-18.253710504808,-16.4360521008819,
1.19077584661778));
#150993=CARTESIAN_POINT('Ctrl Pts',(-18.1716702063162,-16.4545242337241,
1.19494705965951));
#150994=CARTESIAN_POINT('Ctrl Pts',(-18.0896574058363,-16.4729901751342,
1.19911687460703));
#150995=CARTESIAN_POINT('Ctrl Pts',(-18.0085240190108,-16.4955071026302,
1.20328668955455));
#150996=CARTESIAN_POINT('Ctrl Pts',(-17.928693809361,-16.5219625642146,
1.20745650450207));
#150997=CARTESIAN_POINT('Ctrl Pts',(-17.8488664128646,-16.5484170935294,
1.2116261725086));
#150998=CARTESIAN_POINT('Ctrl Pts',(-17.7703425386245,-16.5788097354628,
1.21579584051513));
#150999=CARTESIAN_POINT('Ctrl Pts',(-17.6935296044675,-16.6129785473364,
1.21996550852166));
#151000=CARTESIAN_POINT('Ctrl Pts',(-17.6140201094723,-16.6483468743828,
1.22428155504605));
#151001=CARTESIAN_POINT('Ctrl Pts',(-17.5363443994794,-16.6877612214625,
1.22859760157044));
#151002=CARTESIAN_POINT('Ctrl Pts',(-17.4609286630762,-16.7309891105393,
1.23291364809483));
#151003=CARTESIAN_POINT('Ctrl Pts',(-17.3879657937454,-16.7728110295788,
1.23708931690885));
#151004=CARTESIAN_POINT('Ctrl Pts',(-17.3171185130706,-16.8182019314128,
1.24126498572286));
#151005=CARTESIAN_POINT('Ctrl Pts',(-17.2487433707402,-16.8669070176034,
1.24544065453688));
#151006=CARTESIAN_POINT('Ctrl Pts',(-17.1769202732361,-16.9180681565082,
1.24982688991646));
#151007=CARTESIAN_POINT('Ctrl Pts',(-17.107825650743,-16.972886152708,1.25421312529603));
#151008=CARTESIAN_POINT('Ctrl Pts',(-17.0418318787045,-17.0310192480737,
1.25859936067561));
#151009=CARTESIAN_POINT('Ctrl Pts',(-16.9758381066661,-17.0891523434394,
1.26298559605519));
#151010=CARTESIAN_POINT('Ctrl Pts',(-16.9129455467798,-17.150600078281,
1.26737183143476));
#151011=CARTESIAN_POINT('Ctrl Pts',(-16.8534788456906,-17.2149795084125,
1.27175806681434));
#151012=CARTESIAN_POINT('Ctrl Pts',(-16.7967468035303,-17.2763983609397,
1.2759425950616));
#151013=CARTESIAN_POINT('Ctrl Pts',(-16.7429212561054,-17.3407138418484,
1.28012712330885));
#151014=CARTESIAN_POINT('Ctrl Pts',(-16.6923122163234,-17.4076195436403,
1.28431165155611));
#151015=CARTESIAN_POINT('Ctrl Pts',(-16.6417752336978,-17.4744299850868,
1.2884902218716));
#151016=CARTESIAN_POINT('Ctrl Pts',(-16.5944459372434,-17.5438229582135,
1.29266879218708));
#151017=CARTESIAN_POINT('Ctrl Pts',(-16.550596298851,-17.615456593369,1.29684736250257));
#151018=CARTESIAN_POINT('Ctrl Pts',(-16.5059592554184,-17.6883765489466,
1.30110096712729));
#151019=CARTESIAN_POINT('Ctrl Pts',(-16.4649284015663,-17.7636180793202,
1.30535457175201));
#151020=CARTESIAN_POINT('Ctrl Pts',(-16.4277464893493,-17.840786814058,
1.30960817637672));
#151021=CARTESIAN_POINT('Ctrl Pts',(-16.3912866203068,-17.9164569933187,
1.31377917938137));
#151022=CARTESIAN_POINT('Ctrl Pts',(-16.3585277513987,-17.9939797629346,
1.31795018238601));
#151023=CARTESIAN_POINT('Ctrl Pts',(-16.3296531528721,-18.072957203143,
1.32212118539066));
#151024=CARTESIAN_POINT('Ctrl Pts',(-16.3007882503651,-18.1519081229201,
1.32629078778269));
#151025=CARTESIAN_POINT('Ctrl Pts',(-16.2758051856693,-18.2323123114455,
1.33046039017472));
#151026=CARTESIAN_POINT('Ctrl Pts',(-16.2548387934267,-18.3137526249001,
1.33462999256676));
#151027=CARTESIAN_POINT('Ctrl Pts',(-16.2338731513477,-18.3951900244743,
1.33879944577318));
#151028=CARTESIAN_POINT('Ctrl Pts',(-16.2169240098584,-18.477663029525,
1.3429688989796));
#151029=CARTESIAN_POINT('Ctrl Pts',(-16.2040757430117,-18.5607414487807,
1.34713835218602));
#151030=CARTESIAN_POINT('Ctrl Pts',(-16.1907749845688,-18.6467457324343,
1.3514546456285));
#151031=CARTESIAN_POINT('Ctrl Pts',(-16.181869424783,-18.7333983482173,
1.35577093907098));
#151032=CARTESIAN_POINT('Ctrl Pts',(-16.1773942991259,-18.8202149846984,
1.36008723251346));
#151033=CARTESIAN_POINT('Ctrl Pts',(-16.1730651991088,-18.90419874991,1.36426268309241));
#151034=CARTESIAN_POINT('Ctrl Pts',(-16.1728817996142,-18.9883355251162,
1.36843813367136));
#151035=CARTESIAN_POINT('Ctrl Pts',(-16.1768228581885,-19.0721876258056,
1.37261358425031));
#151036=CARTESIAN_POINT('Ctrl Pts',(-16.1809633215807,-19.1602823716003,
1.37700029912456));
#151037=CARTESIAN_POINT('Ctrl Pts',(-16.1896565615449,-19.2480622945844,
1.3813870139988));
#151038=CARTESIAN_POINT('Ctrl Pts',(-16.2028167371298,-19.3350290978058,
1.38577372887305));
#151039=CARTESIAN_POINT('Ctrl Pts',(-16.2159769127148,-19.4219959010273,
1.39016044374729));
#151040=CARTESIAN_POINT('Ctrl Pts',(-16.2336038329925,-19.5081490310293,
1.39454715862153));
#151041=CARTESIAN_POINT('Ctrl Pts',(-16.2555511525982,-19.593008042705,
1.39893387349578));
#151042=CARTESIAN_POINT('Ctrl Pts',(-16.2764836526239,-19.6739432683273,
1.4031177515669));
#151043=CARTESIAN_POINT('Ctrl Pts',(-16.3014237438776,-19.7540026391425,
1.40730162963803));
#151044=CARTESIAN_POINT('Ctrl Pts',(-16.3302816128663,-19.8327598511259,
1.41148550770915));
#151045=CARTESIAN_POINT('Ctrl Pts',(-16.3591010961105,-19.9114123029754,
1.4156638205296));
#151046=CARTESIAN_POINT('Ctrl Pts',(-16.391827853758,-19.9887656069921,
1.41984213335005));
#151047=CARTESIAN_POINT('Ctrl Pts',(-16.42832166062,-20.0644061287649,1.42402044617049));
#151048=CARTESIAN_POINT('Ctrl Pts',(-16.4647778765757,-20.1399687360639,
1.4281944550671));
#151049=CARTESIAN_POINT('Ctrl Pts',(-16.5049932362158,-20.2138216531577,
1.43236846396371));
#151050=CARTESIAN_POINT('Ctrl Pts',(-16.5487790194524,-20.2855701204566,
1.43654247286032));
#151051=CARTESIAN_POINT('Ctrl Pts',(-16.5925359561236,-20.3572713190599,
1.44071373187301));
#151052=CARTESIAN_POINT('Ctrl Pts',(-16.6398584066156,-20.4268704292796,
1.44488499088571));
#151053=CARTESIAN_POINT('Ctrl Pts',(-16.6905118002526,-20.4939973986662,
1.4490562498984));
#151054=CARTESIAN_POINT('Ctrl Pts',(-16.7411445970495,-20.5610970726761,
1.45322581278081));
#151055=CARTESIAN_POINT('Ctrl Pts',(-16.7951053669189,-20.6257262378605,
1.45739537566322));
#151056=CARTESIAN_POINT('Ctrl Pts',(-16.8521171387588,-20.6875451295102,
1.46156493854563));
#151057=CARTESIAN_POINT('Ctrl Pts',(-16.9091416027605,-20.7493777834998,
1.46573542967084));
#151058=CARTESIAN_POINT('Ctrl Pts',(-16.9692181178399,-20.808398571774,
1.46990592079606));
#151059=CARTESIAN_POINT('Ctrl Pts',(-17.0320310972619,-20.8643027621463,
1.47407641192128));
#151060=CARTESIAN_POINT('Ctrl Pts',(-17.0780839460982,-20.9052902658792,
1.47713410794414));
#151061=CARTESIAN_POINT('Ctrl Pts',(-17.1256069408164,-20.9446031784427,
1.480191803967));
#151062=CARTESIAN_POINT('Ctrl Pts',(-17.1744641402401,-20.9821349467765,
1.48324949998987));
#151063=CARTESIAN_POINT('Origin',(-18.734,-18.952,-1.76670989022851));
#151064=CARTESIAN_POINT('',(-17.1744641402401,-20.9821349467765,2.34989188578132));
#151065=CARTESIAN_POINT('',(-17.1744641402401,-20.9821349467765,2.28327544915889));
#151066=CARTESIAN_POINT('',(-17.1744641402401,-20.9821349467765,-1.76670989022851));
#151067=CARTESIAN_POINT('',(-21.2937660511389,-18.9530076677181,1.83329006740113));
#151068=CARTESIAN_POINT('Ctrl Pts',(-21.293999801981,-18.9530069047618,
1.83329010977149));
#151069=CARTESIAN_POINT('Ctrl Pts',(-21.2940336318731,-18.8669962707737,
1.83754657623943));
#151070=CARTESIAN_POINT('Ctrl Pts',(-21.2897284501564,-18.7810104793984,
1.84180304270736));
#151071=CARTESIAN_POINT('Ctrl Pts',(-21.2811180404876,-18.6955049945465,
1.8460595091753));
#151072=CARTESIAN_POINT('Ctrl Pts',(-21.272502628509,-18.6099498343665,
1.85031844848306));
#151073=CARTESIAN_POINT('Ctrl Pts',(-21.2595770560965,-18.5248759662227,
1.85457738779083));
#151074=CARTESIAN_POINT('Ctrl Pts',(-21.2424267247842,-18.4407316102198,
1.8588363270986));
#151075=CARTESIAN_POINT('Ctrl Pts',(-21.2252479656664,-18.3564477793963,
1.8631023258792));
#151076=CARTESIAN_POINT('Ctrl Pts',(-21.2038305496871,-18.273096962458,
1.8673683246598));
#151077=CARTESIAN_POINT('Ctrl Pts',(-21.1783105998859,-18.191115191842,
1.87163432344041));
#151078=CARTESIAN_POINT('Ctrl Pts',(-21.1527682035212,-18.1090613125802,
1.87590407446243));
#151079=CARTESIAN_POINT('Ctrl Pts',(-21.1231162337396,-18.0283792845701,
1.88017382548446));
#151080=CARTESIAN_POINT('Ctrl Pts',(-21.0895392521437,-17.949485744934,
1.88444357650648));
#151081=CARTESIAN_POINT('Ctrl Pts',(-21.0558918636089,-17.8704267749242,
1.88872228068881));
#151082=CARTESIAN_POINT('Ctrl Pts',(-21.0183032087881,-17.7931641756621,
1.89300098487114));
#151083=CARTESIAN_POINT('Ctrl Pts',(-20.9770042486984,-17.7180907892714,
1.89727968905346));
#151084=CARTESIAN_POINT('Ctrl Pts',(-20.9482314701846,-17.6657875372232,
1.90026064081344));
#151085=CARTESIAN_POINT('Ctrl Pts',(-20.917658721245,-17.614546342522,1.90324159257341));
#151086=CARTESIAN_POINT('Ctrl Pts',(-20.8853760799725,-17.5644910946152,
1.90622254433338));
#151087=CARTESIAN_POINT('Ctrl Pts',(-20.8400579766697,-17.4942239539453,
1.91040717961954));
#151088=CARTESIAN_POINT('Ctrl Pts',(-20.7912093745918,-17.4260486192458,
1.9145918149057));
#151089=CARTESIAN_POINT('Ctrl Pts',(-20.7390496453448,-17.3603417704474,
1.91877645019186));
#151090=CARTESIAN_POINT('Ctrl Pts',(-20.6869641588708,-17.294728447032,
1.92295512917932));
#151091=CARTESIAN_POINT('Ctrl Pts',(-20.6315771902452,-17.2315769876738,
1.92713380816678));
#151092=CARTESIAN_POINT('Ctrl Pts',(-20.5731519433967,-17.1712360827161,
1.93131248715424));
#151093=CARTESIAN_POINT('Ctrl Pts',(-20.5136794819871,-17.1098136269271,
1.9355660648151));
#151094=CARTESIAN_POINT('Ctrl Pts',(-20.4510590117389,-17.05130387858,1.93981964247596));
#151095=CARTESIAN_POINT('Ctrl Pts',(-20.3856118360818,-16.9960403013062,
1.94407322013681));
#151096=CARTESIAN_POINT('Ctrl Pts',(-20.321433464053,-16.9418481014699,
1.94824433503721));
#151097=CARTESIAN_POINT('Ctrl Pts',(-20.2545373771256,-16.8907776413735,
1.9524154499376));
#151098=CARTESIAN_POINT('Ctrl Pts',(-20.1852631886002,-16.8431057026456,
1.956586564838));
#151099=CARTESIAN_POINT('Ctrl Pts',(-20.1160122456088,-16.7954497606359,
1.96075628008586));
#151100=CARTESIAN_POINT('Ctrl Pts',(-20.0443851644975,-16.751190335713,
1.96492599533372));
#151101=CARTESIAN_POINT('Ctrl Pts',(-19.9707522609747,-16.7105621032529,
1.96909571058158));
#151102=CARTESIAN_POINT('Ctrl Pts',(-19.8971219775584,-16.6699353164821,
1.97326527745694));
#151103=CARTESIAN_POINT('Ctrl Pts',(-19.8214864168391,-16.6329396867698,
1.9774348443323));
#151104=CARTESIAN_POINT('Ctrl Pts',(-19.7442411213497,-16.5997642812137,
1.98160441120766));
#151105=CARTESIAN_POINT('Ctrl Pts',(-19.6642800145858,-16.5654224856545,
1.98592057285826));
#151106=CARTESIAN_POINT('Ctrl Pts',(-19.5825943566344,-16.5351747549185,
1.99023673450886));
#151107=CARTESIAN_POINT('Ctrl Pts',(-19.4996442818955,-16.5091760534986,
1.99455289615945));
#151108=CARTESIAN_POINT('Ctrl Pts',(-19.4193962589829,-16.4840242450908,
1.99872846128247));
#151109=CARTESIAN_POINT('Ctrl Pts',(-19.3379653976299,-16.4628489695091,
2.0029040264055));
#151110=CARTESIAN_POINT('Ctrl Pts',(-19.2557808529989,-16.4457388920059,
2.00707959152852));
#151111=CARTESIAN_POINT('Ctrl Pts',(-19.1694454229471,-16.4277646377701,
2.0114660514429));
#151112=CARTESIAN_POINT('Ctrl Pts',(-19.0822787497951,-16.414277123413,
2.01585251135729));
#151113=CARTESIAN_POINT('Ctrl Pts',(-18.9947846786655,-16.4053175794039,
2.02023897127167));
#151114=CARTESIAN_POINT('Ctrl Pts',(-18.9072906075359,-16.3963580353947,
2.02462543118605));
#151115=CARTESIAN_POINT('Ctrl Pts',(-18.8194697217397,-16.3919264150073,
2.02901189110044));
#151116=CARTESIAN_POINT('Ctrl Pts',(-18.7318236815548,-16.3920009250709,
2.03339835101482));
#151117=CARTESIAN_POINT('Ctrl Pts',(-18.6482103252817,-16.3920720068503,
2.03758298542414));
#151118=CARTESIAN_POINT('Ctrl Pts',(-18.5644448542372,-16.3962439324394,
2.04176761983347));
#151119=CARTESIAN_POINT('Ctrl Pts',(-18.4809627381507,-16.4045361348754,
2.04595225424279));
#151120=CARTESIAN_POINT('Ctrl Pts',(-18.3975994484666,-16.4128165343932,
2.05013093234583));
#151121=CARTESIAN_POINT('Ctrl Pts',(-18.3145191664838,-16.4252055165336,
2.05430961044886));
#151122=CARTESIAN_POINT('Ctrl Pts',(-18.2321575527427,-16.4416705080546,
2.0584882885519));
#151123=CARTESIAN_POINT('Ctrl Pts',(-18.1483196667378,-16.4584306226215,
2.06274186643291));
#151124=CARTESIAN_POINT('Ctrl Pts',(-18.0652269487778,-16.4794143083259,
2.06699544431393));
#151125=CARTESIAN_POINT('Ctrl Pts',(-17.983333704675,-16.5045318974371,
2.07124902219494));
#151126=CARTESIAN_POINT('Ctrl Pts',(-17.9030281203276,-16.5291625332492,
2.07542013619884));
#151127=CARTESIAN_POINT('Ctrl Pts',(-17.823876376669,-16.5577680742283,
2.07959125020274));
#151128=CARTESIAN_POINT('Ctrl Pts',(-17.7462950293603,-16.5902127761008,
2.08376236420664));
#151129=CARTESIAN_POINT('Ctrl Pts',(-17.6687397151752,-16.6226465908598,
2.08793207855547));
#151130=CARTESIAN_POINT('Ctrl Pts',(-17.5927541748485,-16.6589168306539,
2.0921017929043));
#151131=CARTESIAN_POINT('Ctrl Pts',(-17.5187361779858,-16.6988391440238,
2.09627150725313));
#151132=CARTESIAN_POINT('Ctrl Pts',(-17.444720814957,-16.7387600368103,
2.10044107322811));
#151133=CARTESIAN_POINT('Ctrl Pts',(-17.3726732606788,-16.7823325256568,
2.1046106392031));
#151134=CARTESIAN_POINT('Ctrl Pts',(-17.3029665902195,-16.8293263604378,
2.10878020517808));
#151135=CARTESIAN_POINT('Ctrl Pts',(-17.230809120241,-16.877972439788,2.11309636788793));
#151136=CARTESIAN_POINT('Ctrl Pts',(-17.161160645027,-16.9302846355734,
2.11741253059778));
#151137=CARTESIAN_POINT('Ctrl Pts',(-17.0944005276118,-16.9859599266179,
2.12172869330762));
#151138=CARTESIAN_POINT('Ctrl Pts',(-17.0298151129941,-17.039821601751,
2.12590425753617));
#151139=CARTESIAN_POINT('Ctrl Pts',(-16.9679330839857,-17.0968302774655,
2.13007982176472));
#151140=CARTESIAN_POINT('Ctrl Pts',(-16.9090612874562,-17.1566730950997,
2.13425538599327));
#151141=CARTESIAN_POINT('Ctrl Pts',(-16.8472160178593,-17.2195384297455,
2.13864184794376));
#151142=CARTESIAN_POINT('Ctrl Pts',(-16.7886934534027,-17.2855312985657,
2.14302830989426));
#151143=CARTESIAN_POINT('Ctrl Pts',(-16.7338009846514,-17.3542503641063,
2.14741477184476));
#151144=CARTESIAN_POINT('Ctrl Pts',(-16.6789085159001,-17.4229694296469,
2.15180123379525));
#151145=CARTESIAN_POINT('Ctrl Pts',(-16.6276464193007,-17.4944141761415,
2.15618769574575));
#151146=CARTESIAN_POINT('Ctrl Pts',(-16.5802679097402,-17.5681509896722,
2.16057415769625));
#151147=CARTESIAN_POINT('Ctrl Pts',(-16.5350693576943,-17.6384950599053,
2.16475879183957));
#151148=CARTESIAN_POINT('Ctrl Pts',(-16.4932366288049,-17.7111867434462,
2.1689434259829));
#151149=CARTESIAN_POINT('Ctrl Pts',(-16.4550217747165,-17.7858703979901,
2.17312806012623));
#151150=CARTESIAN_POINT('Ctrl Pts',(-16.4168613147861,-17.8604477495111,
2.17730673795607));
#151151=CARTESIAN_POINT('Ctrl Pts',(-16.3823087086902,-17.9370110341542,
2.18148541578591));
#151152=CARTESIAN_POINT('Ctrl Pts',(-16.3515723823109,-18.0151762991511,
2.18566409361575));
#151153=CARTESIAN_POINT('Ctrl Pts',(-16.3202851270053,-18.0947426263631,
2.18991767156417));
#151154=CARTESIAN_POINT('Ctrl Pts',(-16.2929525719636,-18.1759685244401,
2.19417124951258));
#151155=CARTESIAN_POINT('Ctrl Pts',(-16.2697452280172,-18.2584234586145,
2.19842482746099));
#151156=CARTESIAN_POINT('Ctrl Pts',(-16.2469878054908,-18.3392798366961,
2.2025959411759));
#151157=CARTESIAN_POINT('Ctrl Pts',(-16.2281972006543,-18.4213175582044,
2.2067670548908));
#151158=CARTESIAN_POINT('Ctrl Pts',(-16.2134847477736,-18.5041128900115,
2.2109381686057));
#151159=CARTESIAN_POINT('Ctrl Pts',(-16.1987772318085,-18.5868804389886,
2.21510788266025));
#151160=CARTESIAN_POINT('Ctrl Pts',(-16.1881452304224,-18.670404640811,
2.2192775967148));
#151161=CARTESIAN_POINT('Ctrl Pts',(-16.1816490383963,-18.7542512482959,
2.22344731076935));
#151162=CARTESIAN_POINT('Ctrl Pts',(-16.1751530775363,-18.8380948721097,
2.22761687644514));
#151163=CARTESIAN_POINT('Ctrl Pts',(-16.1727926681059,-18.9222604200508,
2.23178644212092));
#151164=CARTESIAN_POINT('Ctrl Pts',(-16.1745761446872,-19.0063095650504,
2.23595600779671));
#151165=CARTESIAN_POINT('Ctrl Pts',(-16.1764223263562,-19.0933137861385,
2.24027217084513));
#151166=CARTESIAN_POINT('Ctrl Pts',(-16.1827092038591,-19.1801927391925,
2.24458833389354));
#151167=CARTESIAN_POINT('Ctrl Pts',(-16.1933873263743,-19.2664634201503,
2.24890449694196));
#151168=CARTESIAN_POINT('Ctrl Pts',(-16.2037176087591,-19.3499238313371,
2.25308006086205));
#151169=CARTESIAN_POINT('Ctrl Pts',(-16.218157311486,-19.4328145349867,
2.25725562478214));
#151170=CARTESIAN_POINT('Ctrl Pts',(-16.2366094603544,-19.5147081770231,
2.26143118870224));
#151171=CARTESIAN_POINT('Ctrl Pts',(-16.2559935873087,-19.6007380895988,
2.26581765131481));
#151172=CARTESIAN_POINT('Ctrl Pts',(-16.2798059943325,-19.6856670076961,
2.27020411392739));
#151173=CARTESIAN_POINT('Ctrl Pts',(-16.3078756047366,-19.7690192278691,
2.27459057653996));
#151174=CARTESIAN_POINT('Ctrl Pts',(-16.3359452151407,-19.8523714480422,
2.27897703915253));
#151175=CARTESIAN_POINT('Ctrl Pts',(-16.3682717448823,-19.9341464586679,
2.28336350176511));
#151176=CARTESIAN_POINT('Ctrl Pts',(-16.4046276535555,-20.0138966388589,
2.28774996437768));
#151177=CARTESIAN_POINT('Ctrl Pts',(-16.4393112999405,-20.0899785509834,
2.29193466292291));
#151178=CARTESIAN_POINT('Ctrl Pts',(-16.4777908907529,-20.1645010086698,
2.29611936146814));
#151179=CARTESIAN_POINT('Ctrl Pts',(-16.5199038099267,-20.2370595554693,
2.30030406001337));
#151180=CARTESIAN_POINT('Ctrl Pts',(-16.5619476212891,-20.309499032813,
2.30448189141751));
#151181=CARTESIAN_POINT('Ctrl Pts',(-16.6076126789554,-20.3799806118441,
2.30865972282164));
#151182=CARTESIAN_POINT('Ctrl Pts',(-16.6566890879459,-20.448121443821,
2.31283755422578));
#151183=CARTESIAN_POINT('Ctrl Pts',(-16.7057182446913,-20.516196667752,
2.31701136308798));
#151184=CARTESIAN_POINT('Ctrl Pts',(-16.7581519651898,-20.5819352475649,
2.32118517195017));
#151185=CARTESIAN_POINT('Ctrl Pts',(-16.8137358429733,-20.6449812660625,
2.32535898081237));
#151186=CARTESIAN_POINT('Ctrl Pts',(-16.869286579699,-20.7079896943122,
2.32953030110331));
#151187=CARTESIAN_POINT('Ctrl Pts',(-16.9279834437401,-20.768308402384,
2.33370162139425));
#151188=CARTESIAN_POINT('Ctrl Pts',(-16.9895311180585,-20.8256137061672,
2.33787294168519));
#151189=CARTESIAN_POINT('Ctrl Pts',(-17.0486441410571,-20.8806521747689,
2.3418792563839));
#151190=CARTESIAN_POINT('Ctrl Pts',(-17.1103863961487,-20.9329108595394,
2.34588557108261));
#151191=CARTESIAN_POINT('Ctrl Pts',(-17.1744641402401,-20.9821349467765,
2.34989188578132));
#151192=CARTESIAN_POINT('Ctrl Pts',(-17.173927504734,-20.9828452456383,
1.55000082236257));
#151193=CARTESIAN_POINT('Ctrl Pts',(-17.7189175614377,-21.3927990620285,
1.58395752523188));
#151194=CARTESIAN_POINT('Ctrl Pts',(-19.3278236148535,-21.8312445050739,
1.66030616366168));
#151195=CARTESIAN_POINT('Ctrl Pts',(-21.0477247446925,-20.5363391578402,
1.75473569408639));
#151196=CARTESIAN_POINT('Ctrl Pts',(-21.2914430930582,-19.3178333754147,
1.81520852164178));
#151197=CARTESIAN_POINT('Ctrl Pts',(-21.2901593318677,-18.9530194399495,
1.8332894136367));
#151198=CARTESIAN_POINT('',(-21.2939995273704,-18.9504444089713,1.76670989019937));
#151199=CARTESIAN_POINT('Ctrl Pts',(-17.1744641402401,-20.9821349467765,
1.48324949998987));
#151200=CARTESIAN_POINT('Ctrl Pts',(-17.2411721150464,-21.0333795593612,
1.48742437517027));
#151201=CARTESIAN_POINT('Ctrl Pts',(-17.3103682156612,-21.0813018765702,
1.49159925035068));
#151202=CARTESIAN_POINT('Ctrl Pts',(-17.3816812909535,-21.1256683530757,
1.49577412553108));
#151203=CARTESIAN_POINT('Ctrl Pts',(-17.4530395002482,-21.1700629090974,
1.49995164298747));
#151204=CARTESIAN_POINT('Ctrl Pts',(-17.5265169491212,-21.2108969219799,
1.50412916044385));
#151205=CARTESIAN_POINT('Ctrl Pts',(-17.601718291717,-21.2479830428572,
1.50830667790024));
#151206=CARTESIAN_POINT('Ctrl Pts',(-17.677042648538,-21.2851298291464,
1.51249102893241));
#151207=CARTESIAN_POINT('Ctrl Pts',(-17.7540961057752,-21.3185163049187,
1.51667537996458));
#151208=CARTESIAN_POINT('Ctrl Pts',(-17.8324642291364,-21.348003600551,
1.52085973099674));
#151209=CARTESIAN_POINT('Ctrl Pts',(-17.8652394163241,-21.3603358039081,
1.5226097140569));
#151210=CARTESIAN_POINT('Ctrl Pts',(-17.8982443822024,-21.3719866124526,
1.52435969711706));
#151211=CARTESIAN_POINT('Ctrl Pts',(-17.9314482087024,-21.3829485025983,
1.52610968017722));
#151212=CARTESIAN_POINT('Ctrl Pts',(-18.01084679095,-21.4091611000027,1.53029432359276));
#151213=CARTESIAN_POINT('Ctrl Pts',(-18.0916786888191,-21.4315284615327,
1.53447896700831));
#151214=CARTESIAN_POINT('Ctrl Pts',(-18.1735366063454,-21.4498952708977,
1.53866361042385));
#151215=CARTESIAN_POINT('Ctrl Pts',(-18.2552780145749,-21.4682359385759,
1.54284229778925));
#151216=CARTESIAN_POINT('Ctrl Pts',(-18.3380420967243,-21.4825872643746,
1.54702098515466));
#151217=CARTESIAN_POINT('Ctrl Pts',(-18.4214050302511,-21.4928432428797,
1.55119967252006));
#151218=CARTESIAN_POINT('Ctrl Pts',(-18.5062619503251,-21.5032830236249,
1.5554532481175));
#151219=CARTESIAN_POINT('Ctrl Pts',(-18.5917389405056,-21.5094790670787,
1.55970682371494));
#151220=CARTESIAN_POINT('Ctrl Pts',(-18.6773765369535,-21.5113737092173,
1.56396039931238));
#151221=CARTESIAN_POINT('Ctrl Pts',(-18.7613541250249,-21.513231625409,
1.56813152314313));
#151222=CARTESIAN_POINT('Ctrl Pts',(-18.8454856674055,-21.510953399411,
1.57230264697389));
#151223=CARTESIAN_POINT('Ctrl Pts',(-18.9293330517837,-21.5045369730683,
1.57647377080464));
#151224=CARTESIAN_POINT('Ctrl Pts',(-19.0131523042948,-21.4981226995185,
1.58064349517013));
#151225=CARTESIAN_POINT('Ctrl Pts',(-19.0966871298398,-21.4875730181186,
1.58481321953563));
#151226=CARTESIAN_POINT('Ctrl Pts',(-19.179501972955,-21.4729379191272,
1.58898294390113));
#151227=CARTESIAN_POINT('Ctrl Pts',(-19.2623138727389,-21.4583033402833,
1.59315252007));
#151228=CARTESIAN_POINT('Ctrl Pts',(-19.3444053881076,-21.4395837134394,
1.59732209623888));
#151229=CARTESIAN_POINT('Ctrl Pts',(-19.4253499807632,-21.4168803630397,
1.60149167240775));
#151230=CARTESIAN_POINT('Ctrl Pts',(-19.5091400560411,-21.3933789112856,
1.60580782361199));
#151231=CARTESIAN_POINT('Ctrl Pts',(-19.5917005611986,-21.3656085745896,
1.61012397481624));
#151232=CARTESIAN_POINT('Ctrl Pts',(-19.6725761234496,-21.3337377816398,
1.61444012602048));
#151233=CARTESIAN_POINT('Ctrl Pts',(-19.7508175799528,-21.3029050159575,
1.61861570078383));
#151234=CARTESIAN_POINT('Ctrl Pts',(-19.8274817556368,-21.2682350333859,
1.62279127554719));
#151235=CARTESIAN_POINT('Ctrl Pts',(-19.9021790201189,-21.2299283959234,
1.62696685031055));
#151236=CARTESIAN_POINT('Ctrl Pts',(-19.9806484631081,-21.1896872903713,
1.63135328973523));
#151237=CARTESIAN_POINT('Ctrl Pts',(-20.0569466040008,-21.1454328549357,
1.63573972915991));
#151238=CARTESIAN_POINT('Ctrl Pts',(-20.1306554964563,-21.0974494690434,
1.6401261685846));
#151239=CARTESIAN_POINT('Ctrl Pts',(-20.2043643889117,-21.049466083151,
1.64451260800928));
#151240=CARTESIAN_POINT('Ctrl Pts',(-20.2754836084046,-20.9977541495255,
1.64889904743396));
#151241=CARTESIAN_POINT('Ctrl Pts',(-20.34363649293,-20.9426457144927,1.65328548685865));
#151242=CARTESIAN_POINT('Ctrl Pts',(-20.4078056269716,-20.8907585408379,
1.65741552510087));
#151243=CARTESIAN_POINT('Ctrl Pts',(-20.469597781961,-20.8356563927705,
1.6615455633431));
#151244=CARTESIAN_POINT('Ctrl Pts',(-20.5286666481821,-20.7775880208587,
1.66567560158532));
#151245=CARTESIAN_POINT('Ctrl Pts',(-20.5888757444006,-20.7183987318922,
1.66988536361091));
#151246=CARTESIAN_POINT('Ctrl Pts',(-20.6462548721938,-20.6561277358796,
1.67409512563649));
#151247=CARTESIAN_POINT('Ctrl Pts',(-20.70047016696,-20.5910836105752,1.67830488766208));
#151248=CARTESIAN_POINT('Ctrl Pts',(-20.7535207637169,-20.5274368172154,
1.68242421208196));
#151249=CARTESIAN_POINT('Ctrl Pts',(-20.8035417749399,-20.4611352293305,
1.68654353650185));
#151250=CARTESIAN_POINT('Ctrl Pts',(-20.8502568537434,-20.3925057892921,
1.69066286092173));
#151251=CARTESIAN_POINT('Ctrl Pts',(-20.8969436352055,-20.3239179210705,
1.69477969008884));
#151252=CARTESIAN_POINT('Ctrl Pts',(-20.940328192166,-20.2530053887166,
1.69889651925596));
#151253=CARTESIAN_POINT('Ctrl Pts',(-20.9801755792367,-20.1801267309364,
1.70301334842307));
#151254=CARTESIAN_POINT('Ctrl Pts',(-21.0200115219931,-20.1072690041715,
1.70712899522189));
#151255=CARTESIAN_POINT('Ctrl Pts',(-21.0563120854056,-20.0324466882332,
1.71124464202071));
#151256=CARTESIAN_POINT('Ctrl Pts',(-21.0888874490411,-19.9560443726991,
1.71536028881953));
#151257=CARTESIAN_POINT('Ctrl Pts',(-21.122756810271,-19.8766071129166,
1.71963942226786));
#151258=CARTESIAN_POINT('Ctrl Pts',(-21.1525985823987,-19.7954621912662,
1.72391855571618));
#151259=CARTESIAN_POINT('Ctrl Pts',(-21.1782545829907,-19.7130647367531,
1.7281976891645));
#151260=CARTESIAN_POINT('Ctrl Pts',(-21.2029529666689,-19.6337427887209,
1.73231710284076));
#151261=CARTESIAN_POINT('Ctrl Pts',(-21.2237724306601,-19.5532606399815,
1.73643651651702));
#151262=CARTESIAN_POINT('Ctrl Pts',(-21.2406233757609,-19.4720377410235,
1.74055593019328));
#151263=CARTESIAN_POINT('Ctrl Pts',(-21.257483616485,-19.3907700364207,
1.74467761629503));
#151264=CARTESIAN_POINT('Ctrl Pts',(-21.2703709111432,-19.3087612356736,
1.74879930239678));
#151265=CARTESIAN_POINT('Ctrl Pts',(-21.2792473404998,-19.2264375624415,
1.75292098849853));
#151266=CARTESIAN_POINT('Ctrl Pts',(-21.2881358445687,-19.1440019033387,
1.75704828137884));
#151267=CARTESIAN_POINT('Ctrl Pts',(-21.2930025792327,-19.061250988371,
1.76117557425916));
#151268=CARTESIAN_POINT('Ctrl Pts',(-21.2938616786583,-18.9786117668865,
1.76530286713947));
#151269=CARTESIAN_POINT('Ctrl Pts',(-21.293959302996,-18.969221003687,1.76577187482611));
#151270=CARTESIAN_POINT('Ctrl Pts',(-21.2940052315708,-18.95983167724,1.76624088251274));
#151271=CARTESIAN_POINT('Ctrl Pts',(-21.2939995273704,-18.9504444089713,
1.76670989019937));
#151272=CARTESIAN_POINT('Ctrl Pts',(-21.29399952737,-18.9504444083884,1.7667098902285));
#151273=CARTESIAN_POINT('Ctrl Pts',(-21.2939437779003,-18.8586988530854,
1.77129369133236));
#151274=CARTESIAN_POINT('Ctrl Pts',(-21.2889563823031,-18.7671041917188,
1.77587749243622));
#151275=CARTESIAN_POINT('Ctrl Pts',(-21.2790836671927,-18.6760486872856,
1.78046129354008));
#151276=CARTESIAN_POINT('Ctrl Pts',(-21.2700706759119,-18.5929223680962,
1.78464593362342));
#151277=CARTESIAN_POINT('Ctrl Pts',(-21.2569640808322,-18.5100833893621,
1.78883057370677));
#151278=CARTESIAN_POINT('Ctrl Pts',(-21.2397911341478,-18.4279668025532,
1.79301521379011));
#151279=CARTESIAN_POINT('Ctrl Pts',(-21.2226426307479,-18.3459670972049,
1.79719389762437));
#151280=CARTESIAN_POINT('Ctrl Pts',(-21.2014393656626,-18.2646881878446,
1.80137258145863));
#151281=CARTESIAN_POINT('Ctrl Pts',(-21.1762603194833,-18.1845597535461,
1.80555126529289));
#151282=CARTESIAN_POINT('Ctrl Pts',(-21.1506300008844,-18.1029952143143,
1.80980484174825));
#151283=CARTESIAN_POINT('Ctrl Pts',(-21.1208800336003,-18.0226232755941,
1.81405841820361));
#151284=CARTESIAN_POINT('Ctrl Pts',(-21.0871481586077,-17.9438860463016,
1.81831199465897));
#151285=CARTESIAN_POINT('Ctrl Pts',(-21.0540701842775,-17.866675157493,
1.82248311449243));
#151286=CARTESIAN_POINT('Ctrl Pts',(-21.0171634947162,-17.7910366074843,
1.82665423432589));
#151287=CARTESIAN_POINT('Ctrl Pts',(-20.9766076064455,-17.7173700459194,
1.83082535415935));
#151288=CARTESIAN_POINT('Ctrl Pts',(-20.9360653268187,-17.6437282033794,
1.83499507436165));
#151289=CARTESIAN_POINT('Ctrl Pts',(-20.8918765020354,-17.5720574377846,
1.83916479456395));
#151290=CARTESIAN_POINT('Ctrl Pts',(-20.8442669678557,-17.5027335219578,
1.84333451476625));
#151291=CARTESIAN_POINT('Ctrl Pts',(-20.7966591276122,-17.4334120726597,
1.84750408661088));
#151292=CARTESIAN_POINT('Ctrl Pts',(-20.7456310810944,-17.3664376858416,
1.8516736584555));
#151293=CARTESIAN_POINT('Ctrl Pts',(-20.6914516584179,-17.3021566726028,
1.85584323030013));
#151294=CARTESIAN_POINT('Ctrl Pts',(-20.6353675232618,-17.2356158189659,
1.86015938612691));
#151295=CARTESIAN_POINT('Ctrl Pts',(-20.5759066443104,-17.1719616467127,
1.8644755419537));
#151296=CARTESIAN_POINT('Ctrl Pts',(-20.5134108747745,-17.111538933111,
1.86879169778048));
#151297=CARTESIAN_POINT('Ctrl Pts',(-20.4529507162969,-17.0530843070278,
1.87296726785888));
#151298=CARTESIAN_POINT('Ctrl Pts',(-20.3896507223166,-16.9976541361553,
1.87714283793729));
#151299=CARTESIAN_POINT('Ctrl Pts',(-20.3238547745764,-16.9455200485037,
1.88131840801569));
#151300=CARTESIAN_POINT('Ctrl Pts',(-20.2547359371302,-16.8907530354344,
1.88570485671667));
#151301=CARTESIAN_POINT('Ctrl Pts',(-20.182862878563,-16.8396241326094,
1.89009130541764));
#151302=CARTESIAN_POINT('Ctrl Pts',(-20.1086675044515,-16.7923960427418,
1.89447775411861));
#151303=CARTESIAN_POINT('Ctrl Pts',(-20.03447213034,-16.7451679528743,1.89886420281958));
#151304=CARTESIAN_POINT('Ctrl Pts',(-19.9579549830438,-16.7018408956605,
1.90325065152055));
#151305=CARTESIAN_POINT('Ctrl Pts',(-19.8795742651273,-16.6626202580004,
1.90763710022152));
#151306=CARTESIAN_POINT('Ctrl Pts',(-19.8047997208725,-16.6252041002467,
1.91182173531074));
#151307=CARTESIAN_POINT('Ctrl Pts',(-19.7280509965214,-16.5913855369158,
1.91600637039996));
#151308=CARTESIAN_POINT('Ctrl Pts',(-19.649708651428,-16.5613771385474,
1.92019100548918));
#151309=CARTESIAN_POINT('Ctrl Pts',(-19.5714778164139,-16.5314114532082,
1.92436968429779));
#151310=CARTESIAN_POINT('Ctrl Pts',(-19.4916582921575,-16.5052453236535,
1.9285483631064));
#151311=CARTESIAN_POINT('Ctrl Pts',(-19.4106541203679,-16.4830449170977,
1.93272704191501));
#151312=CARTESIAN_POINT('Ctrl Pts',(-19.3281980247582,-16.4604465890721,
1.93698061962285));
#151313=CARTESIAN_POINT('Ctrl Pts',(-19.2445148259725,-16.4419577675855,
1.94123419733068));
#151314=CARTESIAN_POINT('Ctrl Pts',(-19.1600508251799,-16.4277019402686,
1.94548777503851));
#151315=CARTESIAN_POINT('Ctrl Pts',(-19.0772243047194,-16.4137224867517,
1.94965888980624));
#151316=CARTESIAN_POINT('Ctrl Pts',(-18.9936474609864,-16.4038134443357,
1.95383000457398));
#151317=CARTESIAN_POINT('Ctrl Pts',(-18.9097535040447,-16.3980401910335,
1.95800111934171));
#151318=CARTESIAN_POINT('Ctrl Pts',(-18.8258876980693,-16.3922688749706,
1.96217083447453));
#151319=CARTESIAN_POINT('Ctrl Pts',(-18.7417054487799,-16.3906306234224,
1.96634054960734));
#151320=CARTESIAN_POINT('Ctrl Pts',(-18.6576449613787,-16.3931389431864,
1.97051026474016));
#151321=CARTESIAN_POINT('Ctrl Pts',(-18.5735874647729,-16.3956471737067,
1.97467983151832));
#151322=CARTESIAN_POINT('Ctrl Pts',(-18.4896521812446,-16.4023016676361,
1.97884939829647));
#151323=CARTESIAN_POINT('Ctrl Pts',(-18.4062758154027,-16.4130638332502,
1.98301896507463));
#151324=CARTESIAN_POINT('Ctrl Pts',(-18.319968075054,-16.4242043787278,
1.98733512689366));
#151325=CARTESIAN_POINT('Ctrl Pts',(-18.2342598093425,-16.439746750557,
1.99165128871269));
#151326=CARTESIAN_POINT('Ctrl Pts',(-18.1496259627856,-16.4595901250738,
1.99596745053171));
#151327=CARTESIAN_POINT('Ctrl Pts',(-18.0677490201717,-16.4787871118902,
2.00014301560344));
#151328=CARTESIAN_POINT('Ctrl Pts',(-17.9868780138239,-16.502009022233,
2.00431858067517));
#151329=CARTESIAN_POINT('Ctrl Pts',(-17.9074274756712,-16.5291137331635,
2.0084941457469));
#151330=CARTESIAN_POINT('Ctrl Pts',(-17.8239641319306,-16.5575874207934,
2.01288060593958));
#151331=CARTESIAN_POINT('Ctrl Pts',(-17.7420690633719,-16.590346235575,
2.01726706613225));
#151332=CARTESIAN_POINT('Ctrl Pts',(-17.6621969477419,-16.6271692067657,
2.02165352632493));
#151333=CARTESIAN_POINT('Ctrl Pts',(-17.5823248321119,-16.6639921779565,
2.0260399865176));
#151334=CARTESIAN_POINT('Ctrl Pts',(-17.504476147719,-16.7048789684268,
2.03042644671028));
#151335=CARTESIAN_POINT('Ctrl Pts',(-17.4290716122241,-16.7495554711238,
2.03481290690295));
#151336=CARTESIAN_POINT('Ctrl Pts',(-17.357136554413,-16.7921763397919,
2.03899753937201));
#151337=CARTESIAN_POINT('Ctrl Pts',(-17.2871579127874,-16.8384044871301,
2.04318217184106));
#151338=CARTESIAN_POINT('Ctrl Pts',(-17.2195204149456,-16.8880349841983,
2.04736680431012));
#151339=CARTESIAN_POINT('Ctrl Pts',(-17.1519791912745,-16.9375948379828,
2.05154548043789));
#151340=CARTESIAN_POINT('Ctrl Pts',(-17.086772860019,-16.9905471522445,
2.05572415656566));
#151341=CARTESIAN_POINT('Ctrl Pts',(-17.0242598415601,-17.0466421358133,
2.05990283269343));
#151342=CARTESIAN_POINT('Ctrl Pts',(-16.9606262851279,-17.1037426148895,
2.06415641106388));
#151343=CARTESIAN_POINT('Ctrl Pts',(-16.8997839645222,-17.1640992941634,
2.06840998943434));
#151344=CARTESIAN_POINT('Ctrl Pts',(-16.8420782884877,-17.2274037465225,
2.07266356780479));
#151345=CARTESIAN_POINT('Ctrl Pts',(-16.785491383458,-17.2894808813865,
2.07683467976165));
#151346=CARTESIAN_POINT('Ctrl Pts',(-16.731920908933,-17.3543921535987,
2.08100579171851));
#151347=CARTESIAN_POINT('Ctrl Pts',(-16.6816563258902,-17.4218086906071,
2.08517690367537));
#151348=CARTESIAN_POINT('Ctrl Pts',(-16.6314086098611,-17.4892026050136,
2.08934661595479));
#151349=CARTESIAN_POINT('Ctrl Pts',(-16.5844648568947,-17.5590997461159,
2.09351632823422));
#151350=CARTESIAN_POINT('Ctrl Pts',(-16.5410736162982,-17.6311389642871,
2.09768604051365));
#151351=CARTESIAN_POINT('Ctrl Pts',(-16.4976839199281,-17.7031756186953,
2.10185560439955));
#151352=CARTESIAN_POINT('Ctrl Pts',(-16.4578467211853,-17.7773538040915,
2.10602516828545));
#151353=CARTESIAN_POINT('Ctrl Pts',(-16.4217659505504,-17.8532854326233,
2.11019473217135));
#151354=CARTESIAN_POINT('Ctrl Pts',(-16.3844165855094,-17.9318868056618,
2.1145108972891));
#151355=CARTESIAN_POINT('Ctrl Pts',(-16.3510929501845,-18.0123667456603,
2.11882706240685));
#151356=CARTESIAN_POINT('Ctrl Pts',(-16.3219673471267,-18.094271324093,
2.1231432275246));
#151357=CARTESIAN_POINT('Ctrl Pts',(-16.2937905370921,-18.1735077863526,
2.12731878963606));
#151358=CARTESIAN_POINT('Ctrl Pts',(-16.2695425399181,-18.2540770297308,
2.13149435174752));
#151359=CARTESIAN_POINT('Ctrl Pts',(-16.2493282310178,-18.3355535705167,
2.13566991385898));
#151360=CARTESIAN_POINT('Ctrl Pts',(-16.2280929125411,-18.421145430248,
2.14005638047988));
#151361=CARTESIAN_POINT('Ctrl Pts',(-16.2113095992892,-18.5077380811988,
2.14444284710078));
#151362=CARTESIAN_POINT('Ctrl Pts',(-16.1990385986542,-18.5948296013288,
2.14882931372168));
#151363=CARTESIAN_POINT('Ctrl Pts',(-16.1867675980192,-18.6819211214589,
2.15321578034258));
#151364=CARTESIAN_POINT('Ctrl Pts',(-16.1790088854275,-18.7695109260976,
2.15760224696348));
#151365=CARTESIAN_POINT('Ctrl Pts',(-16.1757597065435,-18.8570968865864,
2.16198871358438));
#151366=CARTESIAN_POINT('Ctrl Pts',(-16.1726599323311,-18.9406554444202,
2.16617348044408));
#151367=CARTESIAN_POINT('Ctrl Pts',(-16.1736525434599,-19.0245215348921,
2.17035824730378));
#151368=CARTESIAN_POINT('Ctrl Pts',(-16.1787734749095,-19.1082606971499,
2.17454301416348));
#151369=CARTESIAN_POINT('Ctrl Pts',(-16.1838870737151,-19.1918799535929,
2.17872178887008));
#151370=CARTESIAN_POINT('Ctrl Pts',(-16.1931172227911,-19.2753721875309,
2.18290056357669));
#151371=CARTESIAN_POINT('Ctrl Pts',(-16.2064478895621,-19.3583007863897,
2.18707933828329));
#151372=CARTESIAN_POINT('Ctrl Pts',(-16.2197626541988,-19.4411304598357,
2.19125312813524));
#151373=CARTESIAN_POINT('Ctrl Pts',(-16.2371681396007,-19.5233973830479,
2.19542691798718));
#151374=CARTESIAN_POINT('Ctrl Pts',(-16.2585964580771,-19.604669368544,
2.19960070783913));
#151375=CARTESIAN_POINT('Ctrl Pts',(-16.2800107743008,-19.685888247172,
2.20377177034406));
#151376=CARTESIAN_POINT('Ctrl Pts',(-16.3054425872083,-19.7661130354452,
2.20794283284899));
#151377=CARTESIAN_POINT('Ctrl Pts',(-16.3347730134509,-19.8449220945941,
2.21211389535393));
#151378=CARTESIAN_POINT('Ctrl Pts',(-16.3640930724252,-19.9237032975281,
2.2162834835358));
#151379=CARTESIAN_POINT('Ctrl Pts',(-16.39730884696,-20.0010693347075,2.22045307171766));
#151380=CARTESIAN_POINT('Ctrl Pts',(-16.4342521400316,-20.0766153922879,
2.22462265989953));
#151381=CARTESIAN_POINT('Ctrl Pts',(-16.4711934569176,-20.152157408728,
2.22879202504011));
#151382=CARTESIAN_POINT('Ctrl Pts',(-16.5118616925174,-20.2258792266091,
2.23296139018068));
#151383=CARTESIAN_POINT('Ctrl Pts',(-16.5560418075785,-20.2973988672747,
2.23713075532125));
#151384=CARTESIAN_POINT('Ctrl Pts',(-16.6002584549483,-20.3689776471614,
2.2413035680883));
#151385=CARTESIAN_POINT('Ctrl Pts',(-16.6479925397301,-20.4383502207137,
2.24547638085536));
#151386=CARTESIAN_POINT('Ctrl Pts',(-16.6989849376185,-20.5051624821249,
2.24964919362241));
#151387=CARTESIAN_POINT('Ctrl Pts',(-16.7499993048254,-20.5720035286083,
2.25382380418396));
#151388=CARTESIAN_POINT('Ctrl Pts',(-16.8042744856599,-20.6362817129064,
2.25799841474552));
#151389=CARTESIAN_POINT('Ctrl Pts',(-16.8615116635141,-20.697676782719,
2.26217302530707));
#151390=CARTESIAN_POINT('Ctrl Pts',(-16.9188352988078,-20.7591645905165,
2.26635394166764));
#151391=CARTESIAN_POINT('Ctrl Pts',(-16.9791295379422,-20.8177602638219,
2.27053485802822));
#151392=CARTESIAN_POINT('Ctrl Pts',(-17.042059662408,-20.8731813797841,
2.27471577438879));
#151393=CARTESIAN_POINT('Ctrl Pts',(-17.0850057020011,-20.9110029709633,
2.27756899931215));
#151394=CARTESIAN_POINT('Ctrl Pts',(-17.1291786179257,-20.9473469165081,
2.28042222423552));
#151395=CARTESIAN_POINT('Ctrl Pts',(-17.1744641402401,-20.9821349467765,
2.28327544915889));
#151396=CARTESIAN_POINT('Origin',(-18.734,-18.952,-1.76670989022851));
#151397=CARTESIAN_POINT('',(-17.1744641402401,-20.9821349467765,3.14981136057519));
#151398=CARTESIAN_POINT('',(-17.1746506047673,-20.9818836121459,3.08342410085253));
#151399=CARTESIAN_POINT('',(-17.1744641402401,-20.9821349467765,-1.76670989022851));
#151400=CARTESIAN_POINT('',(-21.2939989850553,-18.9497204131755,2.63329010980608));
#151401=CARTESIAN_POINT('Ctrl Pts',(-21.2939989850553,-18.9497204131756,
2.63329010980608));
#151402=CARTESIAN_POINT('Ctrl Pts',(-21.2939071256071,-18.8465613267959,
2.63841342883209));
#151403=CARTESIAN_POINT('Ctrl Pts',(-21.287576105512,-18.7436786900576,
2.6435367478581));
#151404=CARTESIAN_POINT('Ctrl Pts',(-21.275128076311,-18.6417289897787,
2.64866006688411));
#151405=CARTESIAN_POINT('Ctrl Pts',(-21.262474961387,-18.538099631808,2.65386779441926));
#151406=CARTESIAN_POINT('Ctrl Pts',(-21.243501668497,-18.4354341184935,
2.65907552195442));
#151407=CARTESIAN_POINT('Ctrl Pts',(-21.2183850428296,-18.3343990293364,
2.66428324948958));
#151408=CARTESIAN_POINT('Ctrl Pts',(-21.2103562166424,-18.3021019691982,
2.66594796113372));
#151409=CARTESIAN_POINT('Ctrl Pts',(-21.2017000060005,-18.2699713447231,
2.66761267277785));
#151410=CARTESIAN_POINT('Ctrl Pts',(-21.1924232051049,-18.2380284707345,
2.66927738442199));
#151411=CARTESIAN_POINT('Ctrl Pts',(-21.1691038390101,-18.1577327328991,
2.67346201883518));
#151412=CARTESIAN_POINT('Ctrl Pts',(-21.1418030734485,-18.078431236944,
2.67764665324838));
#151413=CARTESIAN_POINT('Ctrl Pts',(-21.1106233366666,-18.0005476808522,
2.68183128766158));
#151414=CARTESIAN_POINT('Ctrl Pts',(-21.0794879803785,-17.922774982357,
2.68600996576595));
#151415=CARTESIAN_POINT('Ctrl Pts',(-21.0444847892945,-17.8464166382493,
2.69018864387031));
#151416=CARTESIAN_POINT('Ctrl Pts',(-21.0057661997858,-17.7718820679648,
2.69436732197468));
#151417=CARTESIAN_POINT('Ctrl Pts',(-20.9663536076263,-17.6960115195363,
2.69862089985504));
#151418=CARTESIAN_POINT('Ctrl Pts',(-20.923091244402,-17.6220312333053,
2.70287447773541));
#151419=CARTESIAN_POINT('Ctrl Pts',(-20.876191573922,-17.5503526618234,
2.70712805561577));
#151420=CARTESIAN_POINT('Ctrl Pts',(-20.8302011447859,-17.4800637188824,
2.71129916961465));
#151421=CARTESIAN_POINT('Ctrl Pts',(-20.780713445874,-17.411988443355,2.71547028361353));
#151422=CARTESIAN_POINT('Ctrl Pts',(-20.7279747026929,-17.3464892136704,
2.71964139761241));
#151423=CARTESIAN_POINT('Ctrl Pts',(-20.6752536565045,-17.2810119628825,
2.72381111195386));
#151424=CARTESIAN_POINT('Ctrl Pts',(-20.6192840209004,-17.2181093992113,
2.7279808262953));
#151425=CARTESIAN_POINT('Ctrl Pts',(-20.560353487424,-17.1581123393662,
2.73215054063675));
#151426=CARTESIAN_POINT('Ctrl Pts',(-20.5014250509472,-17.0981174144723,
2.73632010660198));
#151427=CARTESIAN_POINT('Ctrl Pts',(-20.4395362490537,-17.0410281154374,
2.74048967256721));
#151428=CARTESIAN_POINT('Ctrl Pts',(-20.3750119946107,-16.987138774991,
2.74465923853245));
#151429=CARTESIAN_POINT('Ctrl Pts',(-20.3082191477021,-16.9313547524167,
2.74897540124669));
#151430=CARTESIAN_POINT('Ctrl Pts',(-20.2386024799445,-16.879000234265,
2.75329156396094));
#151431=CARTESIAN_POINT('Ctrl Pts',(-20.1665585535975,-16.8303553571546,
2.75760772667519));
#151432=CARTESIAN_POINT('Ctrl Pts',(-20.0968614498203,-16.7832950812909,
2.76178329088814));
#151433=CARTESIAN_POINT('Ctrl Pts',(-20.0248932222052,-16.739706678548,
2.76595885510108));
#151434=CARTESIAN_POINT('Ctrl Pts',(-19.9510397172924,-16.6997978939418,
2.77013441931403));
#151435=CARTESIAN_POINT('Ctrl Pts',(-19.8734560486543,-16.6578734121683,
2.77452088127893));
#151436=CARTESIAN_POINT('Ctrl Pts',(-19.7937921742853,-16.6200102829178,
2.77890734324383));
#151437=CARTESIAN_POINT('Ctrl Pts',(-19.7125190809675,-16.5863921694029,
2.78329380520873));
#151438=CARTESIAN_POINT('Ctrl Pts',(-19.6312459876497,-16.552774055888,
2.78768026717362));
#151439=CARTESIAN_POINT('Ctrl Pts',(-19.5483642476804,-16.5234010802283,
2.79206672913852));
#151440=CARTESIAN_POINT('Ctrl Pts',(-19.464360786173,-16.4983958913426,
2.79645319110342));
#151441=CARTESIAN_POINT('Ctrl Pts',(-19.3842224476364,-16.4745412280211,
2.80063782549363));
#151442=CARTESIAN_POINT('Ctrl Pts',(-19.3027650531602,-16.454572455802,
2.80482245988384));
#151443=CARTESIAN_POINT('Ctrl Pts',(-19.2204003081582,-16.4386327884243,
2.80900709427406));
#151444=CARTESIAN_POINT('Ctrl Pts',(-19.138152799176,-16.4227158091903,
2.81318577235517));
#151445=CARTESIAN_POINT('Ctrl Pts',(-19.0550009527856,-16.4108166300768,
2.81736445043628));
#151446=CARTESIAN_POINT('Ctrl Pts',(-18.9713715368519,-16.403028687197,
2.8215431285174));
#151447=CARTESIAN_POINT('Ctrl Pts',(-18.8862431236693,-16.3951011510316,
2.82579670640354));
#151448=CARTESIAN_POINT('Ctrl Pts',(-18.8006203137754,-16.3914338261787,
2.83005028428969));
#151449=CARTESIAN_POINT('Ctrl Pts',(-18.7149640762876,-16.3920707756642,
2.83430386217583));
#151450=CARTESIAN_POINT('Ctrl Pts',(-18.630968452178,-16.3926953766405,
2.83847497615099));
#151451=CARTESIAN_POINT('Ctrl Pts',(-18.546941166232,-16.3974588441842,
2.84264609012615));
#151452=CARTESIAN_POINT('Ctrl Pts',(-18.4633201985532,-16.4063502901835,
2.84681720410131));
#151453=CARTESIAN_POINT('Ctrl Pts',(-18.3797272906974,-16.4152387525723,
2.85098691841891));
#151454=CARTESIAN_POINT('Ctrl Pts',(-18.296540887401,-16.4282523938205,
2.85515663273652));
#151455=CARTESIAN_POINT('Ctrl Pts',(-18.2141948751358,-16.4453283756812,
2.85932634705412));
#151456=CARTESIAN_POINT('Ctrl Pts',(-18.1318517930947,-16.4624037499053,
2.86349591299542));
#151457=CARTESIAN_POINT('Ctrl Pts',(-18.0503494929033,-16.4835410830848,
2.86766547893671));
#151458=CARTESIAN_POINT('Ctrl Pts',(-17.970111330977,-16.5086264916435,
2.87183504487801));
#151459=CARTESIAN_POINT('Ctrl Pts',(-17.8870520941434,-16.534593872258,
2.87615120762025));
#151460=CARTESIAN_POINT('Ctrl Pts',(-17.8053480471385,-16.5647919650888,
2.88046737036249));
#151461=CARTESIAN_POINT('Ctrl Pts',(-17.7254493921686,-16.5990389566669,
2.88478353310472));
#151462=CARTESIAN_POINT('Ctrl Pts',(-17.6481534275891,-16.6321703560501,
2.88895909729375));
#151463=CARTESIAN_POINT('Ctrl Pts',(-17.5725474425878,-16.6690906702012,
2.89313466148277));
#151464=CARTESIAN_POINT('Ctrl Pts',(-17.4990149692573,-16.7095879116805,
2.8973102256718));
#151465=CARTESIAN_POINT('Ctrl Pts',(-17.4217685453457,-16.752130572642,
2.90169668769064));
#151466=CARTESIAN_POINT('Ctrl Pts',(-17.346811100329,-16.7986206906176,
2.90608314970948));
#151467=CARTESIAN_POINT('Ctrl Pts',(-17.2745520021333,-16.8487616536581,
2.91046961172832));
#151468=CARTESIAN_POINT('Ctrl Pts',(-17.2022929039376,-16.8989026166987,
2.91485607374717));
#151469=CARTESIAN_POINT('Ctrl Pts',(-17.1327325650199,-16.9526940096935,
2.91924253576601));
#151470=CARTESIAN_POINT('Ctrl Pts',(-17.0662376770538,-17.0097927931961,
2.92362899778485));
#151471=CARTESIAN_POINT('Ctrl Pts',(-17.0028023176014,-17.0642643769008,
2.92781363217407));
#151472=CARTESIAN_POINT('Ctrl Pts',(-16.9419203976444,-17.1219484370566,
2.93199826656328));
#151473=CARTESIAN_POINT('Ctrl Pts',(-16.8839351856056,-17.1825763134456,
2.9361829009525));
#151474=CARTESIAN_POINT('Ctrl Pts',(-16.8260325083402,-17.2431178935555,
2.94036157903253));
#151475=CARTESIAN_POINT('Ctrl Pts',(-16.7710186644549,-17.3065946373125,
2.94454025711256));
#151476=CARTESIAN_POINT('Ctrl Pts',(-16.7192032202856,-17.3726982756761,
2.9487189351926));
#151477=CARTESIAN_POINT('Ctrl Pts',(-16.6664590214574,-17.4399867743277,
2.952972513079));
#151478=CARTESIAN_POINT('Ctrl Pts',(-16.6170293785859,-17.5099969539576,
2.95722609096541));
#151479=CARTESIAN_POINT('Ctrl Pts',(-16.5712008555433,-17.5823650629685,
2.96147966885181));
#151480=CARTESIAN_POINT('Ctrl Pts',(-16.5262608079009,-17.6533301748861,
2.96565078282569));
#151481=CARTESIAN_POINT('Ctrl Pts',(-16.4847837540971,-17.7265621993711,
2.96982189679957));
#151482=CARTESIAN_POINT('Ctrl Pts',(-16.4469976092765,-17.8016869709401,
2.97399301077346));
#151483=CARTESIAN_POINT('Ctrl Pts',(-16.4092241439622,-17.8767865336655,
2.97816272508971));
#151484=CARTESIAN_POINT('Ctrl Pts',(-16.3751393344499,-17.9537771714644,
2.98233243940597));
#151485=CARTESIAN_POINT('Ctrl Pts',(-16.3449251982367,-18.0322600413271,
2.98650215372222));
#151486=CARTESIAN_POINT('Ctrl Pts',(-16.3147121371724,-18.1107401184316,
2.9906717196621));
#151487=CARTESIAN_POINT('Ctrl Pts',(-16.2883696400365,-18.1907118923997,
2.99484128560198));
#151488=CARTESIAN_POINT('Ctrl Pts',(-16.2660311035624,-18.2717577444641,
2.99901085154186));
#151489=CARTESIAN_POINT('Ctrl Pts',(-16.2429071716547,-18.355653068883,
3.00332701428556));
#151490=CARTESIAN_POINT('Ctrl Pts',(-16.2240741377505,-18.4406988974033,
3.00764317702926));
#151491=CARTESIAN_POINT('Ctrl Pts',(-16.2096228114113,-18.5264182690326,
3.01195933977297));
#151492=CARTESIAN_POINT('Ctrl Pts',(-16.1956422355373,-18.6093453409713,
3.01613490396041));
#151493=CARTESIAN_POINT('Ctrl Pts',(-16.185762291265,-18.6929022752325,
3.02031046814786));
#151494=CARTESIAN_POINT('Ctrl Pts',(-16.1800123293529,-18.7766518372414,
3.0244860323353));
#151495=CARTESIAN_POINT('Ctrl Pts',(-16.173971950515,-18.8646313908073,
3.02887249435713));
#151496=CARTESIAN_POINT('Ctrl Pts',(-16.172489739197,-18.9528229589758,
3.03325895637896));
#151497=CARTESIAN_POINT('Ctrl Pts',(-16.1755378747839,-19.0407217776812,
3.0376454184008));
#151498=CARTESIAN_POINT('Ctrl Pts',(-16.1785860103708,-19.1286205963865,
3.04203188042263));
#151499=CARTESIAN_POINT('Ctrl Pts',(-16.1861643670755,-19.216226094126,
3.04641834244446));
#151500=CARTESIAN_POINT('Ctrl Pts',(-16.1981829862586,-19.3030442604849,
3.05080480446629));
#151501=CARTESIAN_POINT('Ctrl Pts',(-16.2096452990137,-19.3858438700305,
3.05498823010089));
#151502=CARTESIAN_POINT('Ctrl Pts',(-16.2251885633093,-19.4682355295088,
3.05917165573549));
#151503=CARTESIAN_POINT('Ctrl Pts',(-16.2447727253556,-19.5497855595166,
3.06335508137009));
#151504=CARTESIAN_POINT('Ctrl Pts',(-16.2643314314963,-19.6312295890802,
3.06753306930006));
#151505=CARTESIAN_POINT('Ctrl Pts',(-16.2879205024951,-19.7118337178596,
3.07171105723003));
#151506=CARTESIAN_POINT('Ctrl Pts',(-16.3154483597632,-19.7911709977758,
3.07588904515999));
#151507=CARTESIAN_POINT('Ctrl Pts',(-16.3429486961575,-19.8704289605388,
3.08006285616193));
#151508=CARTESIAN_POINT('Ctrl Pts',(-16.3743798496445,-19.9484221573035,
3.08423666716387));
#151509=CARTESIAN_POINT('Ctrl Pts',(-16.4095998941543,-20.0247367561263,
3.08841047816581));
#151510=CARTESIAN_POINT('Ctrl Pts',(-16.444795294454,-20.1009979560103,
3.09258136866391));
#151511=CARTESIAN_POINT('Ctrl Pts',(-16.4837741268821,-20.1755824748352,
3.09675225916201));
#151512=CARTESIAN_POINT('Ctrl Pts',(-16.5263461035702,-20.2480957810201,
3.10092314966012));
#151513=CARTESIAN_POINT('Ctrl Pts',(-16.5689128842207,-20.3206002367383,
3.10509353108851));
#151514=CARTESIAN_POINT('Ctrl Pts',(-16.6150717177107,-20.3910335782552,
3.10926391251691));
#151515=CARTESIAN_POINT('Ctrl Pts',(-16.6645865127533,-20.4590261506693,
3.1134342939453));
#151516=CARTESIAN_POINT('Ctrl Pts',(-16.7140950873081,-20.5270101812535,
3.1176041514534));
#151517=CARTESIAN_POINT('Ctrl Pts',(-16.7669585097174,-20.5925536836102,
3.12177400896149));
#151518=CARTESIAN_POINT('Ctrl Pts',(-16.8228985547658,-20.6553177231579,
3.12594386646958));
#151519=CARTESIAN_POINT('Ctrl Pts',(-16.8788810408548,-20.7181293810289,
3.13011688759851));
#151520=CARTESIAN_POINT('Ctrl Pts',(-16.9379445036831,-20.7781570213184,
3.13428990872743));
#151521=CARTESIAN_POINT('Ctrl Pts',(-16.9997721932451,-20.8350968945538,
3.13846292985636));
#151522=CARTESIAN_POINT('Ctrl Pts',(-17.0558184987732,-20.886712433719,
3.14224574009597));
#151523=CARTESIAN_POINT('Ctrl Pts',(-17.1141355856602,-20.935790961425,
3.14602855033558));
#151524=CARTESIAN_POINT('Ctrl Pts',(-17.1744641402401,-20.9821349467765,
3.14981136057519));
#151525=CARTESIAN_POINT('Ctrl Pts',(-17.1744641402401,-20.9821349467765,
2.34989188578132));
#151526=CARTESIAN_POINT('Ctrl Pts',(-17.2411525456397,-21.0333645262761,
2.35406142611977));
#151527=CARTESIAN_POINT('Ctrl Pts',(-17.3103704829791,-21.0813066702107,
2.35823096645821));
#151528=CARTESIAN_POINT('Ctrl Pts',(-17.3817556000124,-21.1257145817016,
2.36240050679666));
#151529=CARTESIAN_POINT('Ctrl Pts',(-17.4566943588888,-21.1723331754607,
2.36677761215186));
#151530=CARTESIAN_POINT('Ctrl Pts',(-17.5340212076732,-21.2150562104906,
2.37115471750707));
#151531=CARTESIAN_POINT('Ctrl Pts',(-17.6132860090178,-21.2536516136064,
2.37553182286227));
#151532=CARTESIAN_POINT('Ctrl Pts',(-17.6888991971082,-21.290468983053,
2.37970728138738));
#151533=CARTESIAN_POINT('Ctrl Pts',(-17.7662752668567,-21.3235304882983,
2.38388273991248));
#151534=CARTESIAN_POINT('Ctrl Pts',(-17.8450031383188,-21.3526841899594,
2.38805819843759));
#151535=CARTESIAN_POINT('Ctrl Pts',(-17.9237867046597,-21.3818585159795,
2.39223661082962));
#151536=CARTESIAN_POINT('Ctrl Pts',(-18.003923537627,-21.4071193998067,
2.39641502322166));
#151537=CARTESIAN_POINT('Ctrl Pts',(-18.0849885035953,-21.4283650937482,
2.4005934356137));
#151538=CARTESIAN_POINT('Ctrl Pts',(-18.1661797209869,-21.4496438759549,
2.40477835550876));
#151539=CARTESIAN_POINT('Ctrl Pts',(-18.2483015058921,-21.4668949022888,
2.40896327540382));
#151540=CARTESIAN_POINT('Ctrl Pts',(-18.330920338965,-21.4800677971249,
2.41314819529888));
#151541=CARTESIAN_POINT('Ctrl Pts',(-18.3426179929777,-21.4819328920483,
2.41374072055229));
#151542=CARTESIAN_POINT('Ctrl Pts',(-18.3543256072978,-21.4837163198092,
2.41433324580571));
#151543=CARTESIAN_POINT('Ctrl Pts',(-18.3660419494156,-21.4854180217663,
2.41492577105912));
#151544=CARTESIAN_POINT('Ctrl Pts',(-18.4487871282886,-21.4974360758149,
2.41911040544306));
#151545=CARTESIAN_POINT('Ctrl Pts',(-18.5322757027619,-21.5054183621378,
2.42329503982701));
#151546=CARTESIAN_POINT('Ctrl Pts',(-18.6160795877488,-21.5092826938715,
2.42747967421096));
#151547=CARTESIAN_POINT('Ctrl Pts',(-18.6997641882828,-21.5131415252074,
2.43165835228604));
#151548=CARTESIAN_POINT('Ctrl Pts',(-18.7837627522474,-21.5128940235268,
2.43583703036112));
#151549=CARTESIAN_POINT('Ctrl Pts',(-18.8676394869462,-21.5085094342734,
2.4400157084362));
#151550=CARTESIAN_POINT('Ctrl Pts',(-18.9530196520595,-21.5040462543969,
2.44426928632388));
#151551=CARTESIAN_POINT('Ctrl Pts',(-19.0382731002349,-21.4952961442204,
2.44852286421156));
#151552=CARTESIAN_POINT('Ctrl Pts',(-19.1229373349518,-21.4822821481962,
2.45277644209924));
#151553=CARTESIAN_POINT('Ctrl Pts',(-19.2059601880618,-21.4695204539118,
2.45694755606894));
#151554=CARTESIAN_POINT('Ctrl Pts',(-19.2884159943141,-21.4526587990524,
2.46111867003864));
#151555=CARTESIAN_POINT('Ctrl Pts',(-19.369872949231,-21.4317712782505,
2.46528978400833));
#151556=CARTESIAN_POINT('Ctrl Pts',(-19.4513025704848,-21.4108907664568,
2.4694594983207));
#151557=CARTESIAN_POINT('Ctrl Pts',(-19.5317335608195,-21.3859871858364,
2.47362921263307));
#151558=CARTESIAN_POINT('Ctrl Pts',(-19.6107456770647,-21.3571854435258,
2.47779892694543));
#151559=CARTESIAN_POINT('Ctrl Pts',(-19.6897549817247,-21.3283847261029,
2.48196849288174));
#151560=CARTESIAN_POINT('Ctrl Pts',(-19.7673450807606,-21.2956862811391,
2.48613805881804));
#151561=CARTESIAN_POINT('Ctrl Pts',(-19.8431135302999,-21.2592640024292,
2.49030762475434));
#151562=CARTESIAN_POINT('Ctrl Pts',(-19.9215459053805,-21.2215611611749,
2.49462378750319));
#151563=CARTESIAN_POINT('Ctrl Pts',(-19.9980256738095,-21.179867982504,
2.49893995025204));
#151564=CARTESIAN_POINT('Ctrl Pts',(-20.0721336489206,-21.1344294576518,
2.50325611300089));
#151565=CARTESIAN_POINT('Ctrl Pts',(-20.1438275642521,-21.0904710881423,
2.50743167718557));
#151566=CARTESIAN_POINT('Ctrl Pts',(-20.2133014733427,-21.0430079392832,
2.51160724137025));
#151567=CARTESIAN_POINT('Ctrl Pts',(-20.2802065215959,-20.9923052204448,
2.51578280555493));
#151568=CARTESIAN_POINT('Ctrl Pts',(-20.3504907851974,-20.9390416274994,
2.52016926758587));
#151569=CARTESIAN_POINT('Ctrl Pts',(-20.4179394151666,-20.8822029788409,
2.5245557296168));
#151570=CARTESIAN_POINT('Ctrl Pts',(-20.4821902270813,-20.8221419544883,
2.52894219164774));
#151571=CARTESIAN_POINT('Ctrl Pts',(-20.546441038996,-20.7620809301358,
2.53332865367868));
#151572=CARTESIAN_POINT('Ctrl Pts',(-20.6074936847469,-20.6987980004695,
2.53771511570962));
#151573=CARTESIAN_POINT('Ctrl Pts',(-20.6650349200516,-20.6326856153193,
2.54210157774055));
#151574=CARTESIAN_POINT('Ctrl Pts',(-20.7194682477086,-20.5701440813393,
2.54625111891256));
#151575=CARTESIAN_POINT('Ctrl Pts',(-20.7709705307815,-20.5048282635486,
2.55040066008456));
#151576=CARTESIAN_POINT('Ctrl Pts',(-20.8192426277936,-20.4370465256121,
2.55455020125656));
#151577=CARTESIAN_POINT('Ctrl Pts',(-20.8674506257188,-20.3693547930364,
2.55869423237583));
#151578=CARTESIAN_POINT('Ctrl Pts',(-20.9124366796727,-20.2992040148273,
2.5628382634951));
#151579=CARTESIAN_POINT('Ctrl Pts',(-20.9539402798274,-20.226937313753,
2.56698229461437));
#151580=CARTESIAN_POINT('Ctrl Pts',(-20.9954017278076,-20.1547440086875,
2.57112211694398));
#151581=CARTESIAN_POINT('Ctrl Pts',(-21.0333875106771,-20.0804394498645,
2.57526193927359));
#151582=CARTESIAN_POINT('Ctrl Pts',(-21.0676798966755,-20.0043963796272,
2.5794017616032));
#151583=CARTESIAN_POINT('Ctrl Pts',(-21.1019481578627,-19.9284068059507,
2.5835386715536));
#151584=CARTESIAN_POINT('Ctrl Pts',(-21.1325279904582,-19.8506815753028,
2.58767558150399));
#151585=CARTESIAN_POINT('Ctrl Pts',(-21.1592478841602,-19.771617410977,
2.59181249145439));
#151586=CARTESIAN_POINT('Ctrl Pts',(-21.185962767488,-19.6925680723481,
2.59594862567316));
#151587=CARTESIAN_POINT('Ctrl Pts',(-21.2088189905539,-19.6121807387845,
2.60008475989194));
#151588=CARTESIAN_POINT('Ctrl Pts',(-21.2276938748169,-19.5308703297809,
2.60422089411071));
#151589=CARTESIAN_POINT('Ctrl Pts',(-21.2465668271854,-19.4495682431134,
2.60835660498518));
#151590=CARTESIAN_POINT('Ctrl Pts',(-21.2614591515706,-19.3673437264561,
2.61249231585964));
#151591=CARTESIAN_POINT('Ctrl Pts',(-21.2722989879432,-19.2846232821176,
2.61662802673411));
#151592=CARTESIAN_POINT('Ctrl Pts',(-21.2831447249165,-19.2018578093952,
2.62076598885829));
#151593=CARTESIAN_POINT('Ctrl Pts',(-21.2899335186421,-19.1185963356274,
2.62490395098247));
#151594=CARTESIAN_POINT('Ctrl Pts',(-21.2926453380223,-19.0352708485401,
2.62904191310665));
#151595=CARTESIAN_POINT('Ctrl Pts',(-21.2935733586036,-19.0067557610229,
2.6304579786616));
#151596=CARTESIAN_POINT('Ctrl Pts',(-21.2940243746442,-18.9782331861905,
2.63187404421655));
#151597=CARTESIAN_POINT('Ctrl Pts',(-21.2939989850559,-18.9497204138719,
2.6332901097715));
#151598=CARTESIAN_POINT('',(-21.2939990581247,-18.9541959965425,2.56670989022851));
#151599=CARTESIAN_POINT('Ctrl Pts',(-17.1744641402401,-20.9821349467765,
2.28327544915889));
#151600=CARTESIAN_POINT('Ctrl Pts',(-17.2056206582372,-21.0060691720155,
2.2852384728612));
#151601=CARTESIAN_POINT('Ctrl Pts',(-17.2373036935225,-21.0292671064051,
2.28720149656351));
#151602=CARTESIAN_POINT('Ctrl Pts',(-17.2694745299266,-21.0517059669168,
2.28916452026582));
#151603=CARTESIAN_POINT('Ctrl Pts',(-17.3380540324737,-21.0995395349439,
2.29334915467512));
#151604=CARTESIAN_POINT('Ctrl Pts',(-17.4091070955212,-21.1440987240518,
2.29753378908443));
#151605=CARTESIAN_POINT('Ctrl Pts',(-17.4822878905415,-21.1851181775792,
2.30171842349373));
#151606=CARTESIAN_POINT('Ctrl Pts',(-17.5553645218077,-21.2260792450197,
2.30589710159675));
#151607=CARTESIAN_POINT('Ctrl Pts',(-17.6305624715103,-21.2635103616649,
2.31007577969977));
#151608=CARTESIAN_POINT('Ctrl Pts',(-17.7075059666942,-21.2971886916808,
2.31425445780279));
#151609=CARTESIAN_POINT('Ctrl Pts',(-17.7858286182921,-21.331470681366,
2.31850803568381));
#151610=CARTESIAN_POINT('Ctrl Pts',(-17.8659596132195,-21.3618637479389,
2.32276161356483));
#151611=CARTESIAN_POINT('Ctrl Pts',(-17.947475192358,-21.3881811769579,
2.32701519144585));
#151612=CARTESIAN_POINT('Ctrl Pts',(-18.0274104335102,-21.4139883914482,
2.33118630544973));
#151613=CARTESIAN_POINT('Ctrl Pts',(-18.1086765942978,-21.4358764386359,
2.33535741945361));
#151614=CARTESIAN_POINT('Ctrl Pts',(-18.190854468218,-21.453717995959,2.33952853345749));
#151615=CARTESIAN_POINT('Ctrl Pts',(-18.2730047666085,-21.471553566386,
2.3436982478063));
#151616=CARTESIAN_POINT('Ctrl Pts',(-18.3560657213573,-21.4853452461106,
2.3478679621551));
#151617=CARTESIAN_POINT('Ctrl Pts',(-18.4396056840042,-21.4950163166424,
2.35203767650391));
#151618=CARTESIAN_POINT('Ctrl Pts',(-18.5231426739906,-21.5046870430418,
2.35620724247887));
#151619=CARTESIAN_POINT('Ctrl Pts',(-18.6071581809067,-21.5102373997233,
2.36037680845383));
#151620=CARTESIAN_POINT('Ctrl Pts',(-18.6912145089614,-21.5116424363095,
2.3645463744288));
#151621=CARTESIAN_POINT('Ctrl Pts',(-18.778226152585,-21.5130968722283,
2.36886253713867));
#151622=CARTESIAN_POINT('Ctrl Pts',(-18.8652810139473,-21.5101090568401,
2.37317869984854));
#151623=CARTESIAN_POINT('Ctrl Pts',(-18.9518945613345,-21.5027100893949,
2.37749486255841));
#151624=CARTESIAN_POINT('Ctrl Pts',(-19.0356866828292,-21.4955521424246,
2.38167042678694));
#151625=CARTESIAN_POINT('Ctrl Pts',(-19.1190653399572,-21.4842661264592,
2.38584599101547));
#151626=CARTESIAN_POINT('Ctrl Pts',(-19.2015998086144,-21.4689327402582,
2.390021555244));
#151627=CARTESIAN_POINT('Ctrl Pts',(-19.2883028950858,-21.4528249015418,
2.39440801719454));
#151628=CARTESIAN_POINT('Ctrl Pts',(-19.3740737042372,-21.4322502184737,
2.39879447914509));
#151629=CARTESIAN_POINT('Ctrl Pts',(-19.4584303876454,-21.4073616054374,
2.40318094109563));
#151630=CARTESIAN_POINT('Ctrl Pts',(-19.5427870710536,-21.3824729924011,
2.40756740304617));
#151631=CARTESIAN_POINT('Ctrl Pts',(-19.6257291066931,-21.3532707138335,
2.41195386499671));
#151632=CARTESIAN_POINT('Ctrl Pts',(-19.7068005673137,-21.3199651720906,
2.41634032694725));
#151633=CARTESIAN_POINT('Ctrl Pts',(-19.7841418063303,-21.2881920691418,
2.42052496109048));
#151634=CARTESIAN_POINT('Ctrl Pts',(-19.8600687027268,-21.2525667345391,
2.4247095952337));
#151635=CARTESIAN_POINT('Ctrl Pts',(-19.9341709431478,-21.2132363227278,
2.42889422937693));
#151636=CARTESIAN_POINT('Ctrl Pts',(-20.0081677081176,-21.1739618929342,
2.43307290720666));
#151637=CARTESIAN_POINT('Ctrl Pts',(-20.0803445730473,-21.1309930750319,
2.4372515850364));
#151638=CARTESIAN_POINT('Ctrl Pts',(-20.1503107695072,-21.0845252177121,
2.44143026286614));
#151639=CARTESIAN_POINT('Ctrl Pts',(-20.2215310651425,-21.0372244538674,
2.44568384081458));
#151640=CARTESIAN_POINT('Ctrl Pts',(-20.2904602140006,-20.9862981588784,
2.44993741876302));
#151641=CARTESIAN_POINT('Ctrl Pts',(-20.3567118459237,-20.932001582095,
2.45419099671146));
#151642=CARTESIAN_POINT('Ctrl Pts',(-20.4216790556215,-20.8787576545515,
2.45836211042625));
#151643=CARTESIAN_POINT('Ctrl Pts',(-20.4840712679219,-20.8222732635721,
2.46253322414104));
#151644=CARTESIAN_POINT('Ctrl Pts',(-20.5435545161742,-20.7628319781232,
2.46670433785583));
#151645=CARTESIAN_POINT('Ctrl Pts',(-20.6030178042074,-20.7034106388123,
2.47087405191028));
#151646=CARTESIAN_POINT('Ctrl Pts',(-20.6595737416717,-20.6410347004966,
2.47504376596472));
#151647=CARTESIAN_POINT('Ctrl Pts',(-20.7129241773316,-20.5760255848885,
2.47921348001916));
#151648=CARTESIAN_POINT('Ctrl Pts',(-20.7662727145228,-20.5110187826217,
2.48338304569485));
#151649=CARTESIAN_POINT('Ctrl Pts',(-20.8164156855257,-20.4433793455188,
2.48755261137053));
#151650=CARTESIAN_POINT('Ctrl Pts',(-20.8630951945853,-20.3734618012432,
2.49172217704622));
#151651=CARTESIAN_POINT('Ctrl Pts',(-20.9114159041743,-20.3010860325135,
2.49603834009476));
#151652=CARTESIAN_POINT('Ctrl Pts',(-20.9560247758173,-20.226269417489,
2.5003545031433));
#151653=CARTESIAN_POINT('Ctrl Pts',(-20.9966856911225,-20.1494362042253,
2.50467066619184));
#151654=CARTESIAN_POINT('Ctrl Pts',(-21.036022076007,-20.0751058349709,
2.50884623011182));
#151655=CARTESIAN_POINT('Ctrl Pts',(-21.0716636082435,-19.9988886784647,
2.5130217940318));
#151656=CARTESIAN_POINT('Ctrl Pts',(-21.1034449999269,-19.9211905861704,
2.51719735795179));
#151657=CARTESIAN_POINT('Ctrl Pts',(-21.1368316008925,-19.839568131463,
2.52158382056461));
#151658=CARTESIAN_POINT('Ctrl Pts',(-21.1659576672678,-19.756311755636,
2.52597028317742));
#151659=CARTESIAN_POINT('Ctrl Pts',(-21.1906909603509,-19.6719093868885,
2.53035674579024));
#151660=CARTESIAN_POINT('Ctrl Pts',(-21.215424253434,-19.5875070181411,
2.53474320840306));
#151661=CARTESIAN_POINT('Ctrl Pts',(-21.2357647130118,-19.5019592385496,
2.53912967101588));
#151662=CARTESIAN_POINT('Ctrl Pts',(-21.2516424693651,-19.4157632978678,
2.54351613362869));
#151663=CARTESIAN_POINT('Ctrl Pts',(-21.2744558895146,-19.2919155598001,
2.54981867489014));
#151664=CARTESIAN_POINT('Ctrl Pts',(-21.2881358177162,-19.1663368452798,
2.55612121615159));
#151665=CARTESIAN_POINT('Ctrl Pts',(-21.2924829866165,-19.0401181433864,
2.56242375741304));
#151666=CARTESIAN_POINT('Ctrl Pts',(-21.2934684379609,-19.0115058689788,
2.56385246835153));
#151667=CARTESIAN_POINT('Ctrl Pts',(-21.2939744691011,-18.982860830915,
2.56528117929002));
#151668=CARTESIAN_POINT('Ctrl Pts',(-21.2939990581247,-18.9541959965425,
2.56670989022851));
#151669=CARTESIAN_POINT('Ctrl Pts',(-21.2953147714723,-18.9541844553181,
2.56671052139392));
#151670=CARTESIAN_POINT('Ctrl Pts',(-21.288986792687,-18.2584132339351,
2.60137099436598));
#151671=CARTESIAN_POINT('Ctrl Pts',(-20.6359183782719,-16.7012242333178,
2.67842340289853));
#151672=CARTESIAN_POINT('Ctrl Pts',(-18.0006016698944,-16.0150938498363,
2.79786774699156));
#151673=CARTESIAN_POINT('Ctrl Pts',(-15.8675520976762,-17.9789803420861,
2.92504355367299));
#151674=CARTESIAN_POINT('Ctrl Pts',(-16.2393388133108,-20.1169975231494,
3.02022900495998));
#151675=CARTESIAN_POINT('Ctrl Pts',(-17.007518734373,-20.85614290823,3.0730225206865));
#151676=CARTESIAN_POINT('Ctrl Pts',(-17.1746506047676,-20.9818836121461,
3.08342410085255));
#151677=CARTESIAN_POINT('Origin',(-18.734,-18.952,-1.76670989022851));
#151678=CARTESIAN_POINT('',(-17.1744641402401,-20.9821349467765,3.94993168147533));
#151679=CARTESIAN_POINT('',(-17.1744641402401,-20.9821349467765,3.88329344502913));
#151680=CARTESIAN_POINT('',(-17.1744641402401,-20.9821349467765,-1.76670989022851));
#151681=CARTESIAN_POINT('',(-21.2939999971965,-18.9521198080496,3.43329010980363));
#151682=CARTESIAN_POINT('Ctrl Pts',(-21.2939999971965,-18.9521198080496,
3.43329010980363));
#151683=CARTESIAN_POINT('Ctrl Pts',(-21.294003905102,-18.8686175883755,
3.43746913841141));
#151684=CARTESIAN_POINT('Ctrl Pts',(-21.2899179933662,-18.784957797327,
3.44164816701919));
#151685=CARTESIAN_POINT('Ctrl Pts',(-21.2817219740999,-18.7015748760837,
3.44582719562697));
#151686=CARTESIAN_POINT('Ctrl Pts',(-21.2735376207105,-18.6183106386626,
3.45000027597723));
#151687=CARTESIAN_POINT('Ctrl Pts',(-21.2612548239782,-18.5353229435677,
3.45417335632749));
#151688=CARTESIAN_POINT('Ctrl Pts',(-21.2449053023278,-18.4530465324881,
3.45834643667775));
#151689=CARTESIAN_POINT('Ctrl Pts',(-21.228391285294,-18.3699423241145,
3.46256150311585));
#151690=CARTESIAN_POINT('Ctrl Pts',(-21.2077282378307,-18.287564271427,
3.46677656955394));
#151691=CARTESIAN_POINT('Ctrl Pts',(-21.1830026840864,-18.2063554108441,
3.47099163599204));
#151692=CARTESIAN_POINT('Ctrl Pts',(-21.1585674190593,-18.1260999774808,
3.47515721572331));
#151693=CARTESIAN_POINT('Ctrl Pts',(-21.1301646741428,-18.0469868800103,
3.47932279545459));
#151694=CARTESIAN_POINT('Ctrl Pts',(-21.0979289771719,-17.9694320426113,
3.48348837518587));
#151695=CARTESIAN_POINT('Ctrl Pts',(-21.0657039544922,-17.8919028861496,
3.48765257555777));
#151696=CARTESIAN_POINT('Ctrl Pts',(-21.0296486772609,-17.815931390789,
3.49181677592968));
#151697=CARTESIAN_POINT('Ctrl Pts',(-20.9899463178963,-17.7419147919381,
3.49598097630159));
#151698=CARTESIAN_POINT('Ctrl Pts',(-20.9502451090693,-17.6679003380199,
3.50014505599882));
#151699=CARTESIAN_POINT('Ctrl Pts',(-20.9068972472216,-17.5958410741357,
3.50430913569606));
#151700=CARTESIAN_POINT('Ctrl Pts',(-20.8601318431732,-17.5261096166098,
3.50847321539329));
#151701=CARTESIAN_POINT('Ctrl Pts',(-20.8123689128482,-17.4548907569624,
3.51272611670985));
#151702=CARTESIAN_POINT('Ctrl Pts',(-20.7610412266544,-17.3861005826242,
3.51697901802641));
#151703=CARTESIAN_POINT('Ctrl Pts',(-20.7064383509254,-17.3201032655836,
3.52123191934298));
#151704=CARTESIAN_POINT('Ctrl Pts',(-20.6528987388226,-17.2553910923328,
3.52540200532764));
#151705=CARTESIAN_POINT('Ctrl Pts',(-20.5962107113946,-17.1933642853479,
3.52957209131231));
#151706=CARTESIAN_POINT('Ctrl Pts',(-20.5366855500211,-17.1343298407728,
3.53374217729697));
#151707=CARTESIAN_POINT('Ctrl Pts',(-20.4753871892412,-17.0735368147901,
3.53803648627948));
#151708=CARTESIAN_POINT('Ctrl Pts',(-20.4110803806519,-17.0159176096093,
3.54233079526199));
#151709=CARTESIAN_POINT('Ctrl Pts',(-20.344141220394,-16.9617625140732,
3.5466251042445));
#151710=CARTESIAN_POINT('Ctrl Pts',(-20.277202060136,-16.9076074185371,
3.55091941322701));
#151711=CARTESIAN_POINT('Ctrl Pts',(-20.2076310154015,-16.8569166856669,
3.55521372220952));
#151712=CARTESIAN_POINT('Ctrl Pts',(-20.1358342086541,-16.8099307080659,
3.55950803119203));
#151713=CARTESIAN_POINT('Ctrl Pts',(-20.065871057879,-16.7641447297733,
3.56369266558497));
#151714=CARTESIAN_POINT('Ctrl Pts',(-19.9935321931096,-16.7217048000893,
3.56787729997791));
#151715=CARTESIAN_POINT('Ctrl Pts',(-19.9191711337668,-16.6828659396841,
3.57206193437085));
#151716=CARTESIAN_POINT('Ctrl Pts',(-19.844915918188,-16.6440823615894,
3.57624061245468));
#151717=CARTESIAN_POINT('Ctrl Pts',(-19.7686446296087,-16.6088898827212,
3.58041929053851));
#151718=CARTESIAN_POINT('Ctrl Pts',(-19.6907394622033,-16.5775001365629,
3.58459796862235));
#151719=CARTESIAN_POINT('Ctrl Pts',(-19.6114379006591,-16.545547751763,
3.58885154650781));
#151720=CARTESIAN_POINT('Ctrl Pts',(-19.5304437130242,-16.5175360325718,
3.59310512439327));
#151721=CARTESIAN_POINT('Ctrl Pts',(-19.4481859912091,-16.4936390887503,
3.59735870227873));
#151722=CARTESIAN_POINT('Ctrl Pts',(-19.3675229958469,-16.4702054338166,
3.60152981625657));
#151723=CARTESIAN_POINT('Ctrl Pts',(-19.2856454833717,-16.4507285663624,
3.60570093023441));
#151724=CARTESIAN_POINT('Ctrl Pts',(-19.202976239882,-16.4353233647474,
3.60987204421224));
#151725=CARTESIAN_POINT('Ctrl Pts',(-19.1203347368553,-16.4199233324967,
3.6140417585325));
#151726=CARTESIAN_POINT('Ctrl Pts',(-19.0369024823163,-16.408592336823,
3.61821147285276));
#151727=CARTESIAN_POINT('Ctrl Pts',(-18.9531132034112,-16.4013943064262,
3.62238118717302));
#151728=CARTESIAN_POINT('Ctrl Pts',(-18.8693269060884,-16.3941965321663,
3.62655075311695));
#151729=CARTESIAN_POINT('Ctrl Pts',(-18.785184068077,-16.3911314692988,
3.63072031906087));
#151730=CARTESIAN_POINT('Ctrl Pts',(-18.7011229313377,-16.3922111223079,
3.6348898850048));
#151731=CARTESIAN_POINT('Ctrl Pts',(-18.6141063087261,-16.393328734585,
3.63920604774385));
#151732=CARTESIAN_POINT('Ctrl Pts',(-18.5271777668962,-16.3988879352091,
3.6435222104829));
#151733=CARTESIAN_POINT('Ctrl Pts',(-18.4408207068908,-16.4088433193977,
3.64783837322196));
#151734=CARTESIAN_POINT('Ctrl Pts',(-18.3572767190368,-16.418474407993,
3.65201393741352));
#151735=CARTESIAN_POINT('Ctrl Pts',(-18.274268009732,-16.4322195436239,
3.65618950160509));
#151736=CARTESIAN_POINT('Ctrl Pts',(-18.1922227301015,-16.4499853338117,
3.66036506579665));
#151737=CARTESIAN_POINT('Ctrl Pts',(-18.1060335384336,-16.4686484318293,
3.66475152780945));
#151738=CARTESIAN_POINT('Ctrl Pts',(-18.0209082233737,-16.4917488722623,
3.66913798982225));
#151739=CARTESIAN_POINT('Ctrl Pts',(-17.9373239039192,-16.5191195676866,
3.67352445183505));
#151740=CARTESIAN_POINT('Ctrl Pts',(-17.8537395844646,-16.5464902631109,
3.67791091384785));
#151741=CARTESIAN_POINT('Ctrl Pts',(-17.7716967745984,-16.578130933778,
3.68229737586065));
#151742=CARTESIAN_POINT('Ctrl Pts',(-17.6916449845523,-16.6138177954293,
3.68668383787346));
#151743=CARTESIAN_POINT('Ctrl Pts',(-17.6152764960369,-16.647862651673,
3.69086847226646));
#151744=CARTESIAN_POINT('Ctrl Pts',(-17.5404355759515,-16.6857162600702,
3.69505310665946));
#151745=CARTESIAN_POINT('Ctrl Pts',(-17.4675280096795,-16.7272194045853,
3.69923774105246));
#151746=CARTESIAN_POINT('Ctrl Pts',(-17.394724218304,-16.7686634745113,
3.70341641913635));
#151747=CARTESIAN_POINT('Ctrl Pts',(-17.3238487109969,-16.813746536681,
3.70759509722024));
#151748=CARTESIAN_POINT('Ctrl Pts',(-17.2552863124839,-16.8622617794679,
3.71177377530414));
#151749=CARTESIAN_POINT('Ctrl Pts',(-17.1854949822514,-16.9116466231152,
3.71602735318959));
#151750=CARTESIAN_POINT('Ctrl Pts',(-17.1181009417722,-16.9645877049941,
3.72028093107504));
#151751=CARTESIAN_POINT('Ctrl Pts',(-17.0534828491147,-17.0208184690246,
3.72453450896048));
#151752=CARTESIAN_POINT('Ctrl Pts',(-16.9901175042762,-17.0759590899683,
3.72870562293838));
#151753=CARTESIAN_POINT('Ctrl Pts',(-16.9294217964547,-17.1342626616187,
3.73287673691628));
#151754=CARTESIAN_POINT('Ctrl Pts',(-16.8717211662673,-17.1954358692518,
3.73704785089418));
#151755=CARTESIAN_POINT('Ctrl Pts',(-16.8140398980835,-17.2565885496243,
3.7412175652145));
#151756=CARTESIAN_POINT('Ctrl Pts',(-16.7593520269263,-17.3206086192035,
3.74538727953482));
#151757=CARTESIAN_POINT('Ctrl Pts',(-16.7079460749934,-17.3871659854907,
3.74955699385514));
#151758=CARTESIAN_POINT('Ctrl Pts',(-16.6565419523049,-17.4537209833811,
3.75372655979912));
#151759=CARTESIAN_POINT('Ctrl Pts',(-16.6084197971694,-17.5228127338604,
3.75789612574311));
#151760=CARTESIAN_POINT('Ctrl Pts',(-16.5638269155198,-17.5940792425927,
3.76206569168709));
#151761=CARTESIAN_POINT('Ctrl Pts',(-16.5176662031612,-17.6678513938575,
3.76638185442608));
#151762=CARTESIAN_POINT('Ctrl Pts',(-16.4752878401623,-17.7439536306547,
3.77069801716506));
#151763=CARTESIAN_POINT('Ctrl Pts',(-16.4369153041026,-17.8219549124597,
3.77501417990404));
#151764=CARTESIAN_POINT('Ctrl Pts',(-16.39979274937,-17.8974153107121,3.77918974409566));
#151765=CARTESIAN_POINT('Ctrl Pts',(-16.3664191932587,-17.9746524800457,
3.78336530828728));
#151766=CARTESIAN_POINT('Ctrl Pts',(-16.3369478575573,-18.0532558615431,
3.78754087247891));
#151767=CARTESIAN_POINT('Ctrl Pts',(-16.3059879947497,-18.1358293129816,
3.79192733449157));
#151768=CARTESIAN_POINT('Ctrl Pts',(-16.2793350909185,-18.2199100618433,
3.79631379650423));
#151769=CARTESIAN_POINT('Ctrl Pts',(-16.2571069074461,-18.3050064853038,
3.8007002585169));
#151770=CARTESIAN_POINT('Ctrl Pts',(-16.2348787239738,-18.3901029087642,
3.80508672052956));
#151771=CARTESIAN_POINT('Ctrl Pts',(-16.2170753038452,-18.4762144232225,
3.80947318254223));
#151772=CARTESIAN_POINT('Ctrl Pts',(-16.2037517912764,-18.5628419315354,
3.81385964455489));
#151773=CARTESIAN_POINT('Ctrl Pts',(-16.1910413132713,-18.645483579777,
3.818044278948));
#151774=CARTESIAN_POINT('Ctrl Pts',(-16.182360236898,-18.7289023900138,
3.82222891334111));
#151775=CARTESIAN_POINT('Ctrl Pts',(-16.1777943305987,-18.812670980335,
3.82641354773422));
#151776=CARTESIAN_POINT('Ctrl Pts',(-16.1732349233019,-18.8963203364362,
3.83059222581821));
#151777=CARTESIAN_POINT('Ctrl Pts',(-16.1727790761929,-18.9803180282759,
3.83477090390221));
#151778=CARTESIAN_POINT('Ctrl Pts',(-16.1764611917473,-19.0642285359488,
3.83894958198621));
#151779=CARTESIAN_POINT('Ctrl Pts',(-16.1802093065766,-19.149643079165,
3.84320315987163));
#151780=CARTESIAN_POINT('Ctrl Pts',(-16.1882452624471,-19.2349668053833,
3.84745673775705));
#151781=CARTESIAN_POINT('Ctrl Pts',(-16.2005498883094,-19.3197370413416,
3.85171031564247));
#151782=CARTESIAN_POINT('Ctrl Pts',(-16.212615964989,-19.4028638408618,
3.85588142962048));
#151783=CARTESIAN_POINT('Ctrl Pts',(-16.2287866065492,-19.4854579433574,
3.86005254359849));
#151784=CARTESIAN_POINT('Ctrl Pts',(-16.2489913365583,-19.5670869390743,
3.8642236575765));
#151785=CARTESIAN_POINT('Ctrl Pts',(-16.2691892866752,-19.6486885433934,
3.86839337189693));
#151786=CARTESIAN_POINT('Ctrl Pts',(-16.293418526377,-19.7293252379216,
3.87256308621737));
#151787=CARTESIAN_POINT('Ctrl Pts',(-16.3215576717042,-19.8085757483414,
3.8767328005378));
#151788=CARTESIAN_POINT('Ctrl Pts',(-16.3496958157198,-19.887823438688,
3.8809023664819));
#151789=CARTESIAN_POINT('Ctrl Pts',(-16.3817434340021,-19.9656846097681,
3.885071932426));
#151790=CARTESIAN_POINT('Ctrl Pts',(-16.4175300086122,-20.041755375761,
3.8892414983701));
#151791=CARTESIAN_POINT('Ctrl Pts',(-16.454574795037,-20.1205006960403,
3.89355766110895));
#151792=CARTESIAN_POINT('Ctrl Pts',(-16.4956261286208,-20.1973268901832,
3.8978738238478));
#151793=CARTESIAN_POINT('Ctrl Pts',(-16.5404425366711,-20.2718127348508,
3.90218998658666));
#151794=CARTESIAN_POINT('Ctrl Pts',(-16.5837990549444,-20.3438722109649,
3.9063655507784));
#151795=CARTESIAN_POINT('Ctrl Pts',(-16.6306788183652,-20.4137411050174,
3.91054111497014));
#151796=CARTESIAN_POINT('Ctrl Pts',(-16.6808195479046,-20.4810683539769,
3.91471667916187));
#151797=CARTESIAN_POINT('Ctrl Pts',(-16.7334927664925,-20.5517961422228,
3.91910314117428));
#151798=CARTESIAN_POINT('Ctrl Pts',(-16.7897646588838,-20.619718331068,
3.92348960318669));
#151799=CARTESIAN_POINT('Ctrl Pts',(-16.849285590087,-20.6844697957155,
3.9278760651991));
#151800=CARTESIAN_POINT('Ctrl Pts',(-16.9088065212902,-20.749221260363,
3.93226252721151));
#151801=CARTESIAN_POINT('Ctrl Pts',(-16.9715760238563,-20.8108016487771,
3.93664898922392));
#151802=CARTESIAN_POINT('Ctrl Pts',(-17.0372042845901,-20.8688944415816,
3.94103545123633));
#151803=CARTESIAN_POINT('Ctrl Pts',(-17.0815714090152,-20.9081673118016,
3.944000861316));
#151804=CARTESIAN_POINT('Ctrl Pts',(-17.1273611506995,-20.945950750545,
3.94696627139566));
#151805=CARTESIAN_POINT('Ctrl Pts',(-17.1744641402401,-20.9821349467765,
3.94993168147533));
#151806=CARTESIAN_POINT('Ctrl Pts',(-17.1744641402401,-20.9821349467765,
3.14981136057519));
#151807=CARTESIAN_POINT('Ctrl Pts',(-17.2410960571067,-21.0333211321692,
3.15398941355794));
#151808=CARTESIAN_POINT('Ctrl Pts',(-17.3101818003053,-21.081170625289,
3.15816746654069));
#151809=CARTESIAN_POINT('Ctrl Pts',(-17.3813457473345,-21.1254595631725,
3.16234551952344));
#151810=CARTESIAN_POINT('Ctrl Pts',(-17.4526225822357,-21.169818756911,
3.16653020018116));
#151811=CARTESIAN_POINT('Ctrl Pts',(-17.5259837968862,-21.2106059047489,
3.17071488083887));
#151812=CARTESIAN_POINT('Ctrl Pts',(-17.6010303509287,-21.2476436514153,
3.17489956149659));
#151813=CARTESIAN_POINT('Ctrl Pts',(-17.619448495431,-21.2567335633885,
3.17592657804697));
#151814=CARTESIAN_POINT('Ctrl Pts',(-17.6379680672954,-21.2655978709631,
3.17695359459734));
#151815=CARTESIAN_POINT('Ctrl Pts',(-17.6565830150582,-21.2742344068933,
3.17798061114772));
#151816=CARTESIAN_POINT('Ctrl Pts',(-17.7324306249074,-21.3094244389056,
3.18216524554016));
#151817=CARTESIAN_POINT('Ctrl Pts',(-17.8101452346756,-21.3409601078314,
3.1863498799326));
#151818=CARTESIAN_POINT('Ctrl Pts',(-17.8893401694871,-21.3686401823023,
3.19053451432505));
#151819=CARTESIAN_POINT('Ctrl Pts',(-17.9684223801111,-21.3962808576132,
3.19471319240838));
#151820=CARTESIAN_POINT('Ctrl Pts',(-18.0489802999385,-21.4200766888001,
3.19889187049172));
#151821=CARTESIAN_POINT('Ctrl Pts',(-18.1306051532973,-21.4398735214984,
3.20307054857505));
#151822=CARTESIAN_POINT('Ctrl Pts',(-18.2136930735049,-21.4600251981987,
3.20732412646064));
#151823=CARTESIAN_POINT('Ctrl Pts',(-18.2978861156728,-21.4760328992745,
3.21157770434623));
#151824=CARTESIAN_POINT('Ctrl Pts',(-18.3827345240936,-21.4877863800873,
3.21583128223182));
#151825=CARTESIAN_POINT('Ctrl Pts',(-18.4659379805339,-21.4993119967375,
3.22000239620916));
#151826=CARTESIAN_POINT('Ctrl Pts',(-18.5497711422166,-21.5067468078098,
3.2241735101865));
#151827=CARTESIAN_POINT('Ctrl Pts',(-18.633799056368,-21.5100382661124,
3.22834462416384));
#151828=CARTESIAN_POINT('Ctrl Pts',(-18.7177987741413,-21.5133286199344,
3.2325143384836));
#151829=CARTESIAN_POINT('Ctrl Pts',(-18.8019926552973,-21.5124783642369,
3.23668405280337));
#151830=CARTESIAN_POINT('Ctrl Pts',(-18.8859422870026,-21.5074869480043,
3.24085376712313));
#151831=CARTESIAN_POINT('Ctrl Pts',(-18.9698889314197,-21.5024957093878,
3.24502333306657));
#151832=CARTESIAN_POINT('Ctrl Pts',(-19.0535908844956,-21.493363631381,
3.24919289901));
#151833=CARTESIAN_POINT('Ctrl Pts',(-19.136612772952,-21.4801421943902,
3.25336246495344));
#151834=CARTESIAN_POINT('Ctrl Pts',(-19.2225536086148,-21.4664559079808,
3.25767862769308));
#151835=CARTESIAN_POINT('Ctrl Pts',(-19.3077651468766,-21.4483874314134,
3.26199479043273));
#151836=CARTESIAN_POINT('Ctrl Pts',(-19.3917756297608,-21.4260515800793,
3.26631095317237));
#151837=CARTESIAN_POINT('Ctrl Pts',(-19.473049479976,-21.4044433167598,
3.27048651736345));
#151838=CARTESIAN_POINT('Ctrl Pts',(-19.5531988875818,-21.3788416169569,
3.27466208155453));
#151839=CARTESIAN_POINT('Ctrl Pts',(-19.6318137018706,-21.3494007918438,
3.27883764574561));
#151840=CARTESIAN_POINT('Ctrl Pts',(-19.7143991635781,-21.3184729806291,
3.28322410775954));
#151841=CARTESIAN_POINT('Ctrl Pts',(-19.7952903977544,-21.2833082561225,
3.28761056977346));
#151842=CARTESIAN_POINT('Ctrl Pts',(-19.8740394547189,-21.2441409297171,
3.29199703178738));
#151843=CARTESIAN_POINT('Ctrl Pts',(-19.9527885116833,-21.2049736033117,
3.29638349380131));
#151844=CARTESIAN_POINT('Ctrl Pts',(-20.0293949232976,-21.161804026126,
3.30076995581523));
#151845=CARTESIAN_POINT('Ctrl Pts',(-20.103446255522,-21.1149186191895,
3.30515641782916));
#151846=CARTESIAN_POINT('Ctrl Pts',(-20.1740903761505,-21.070190479346,
3.30934105222176));
#151847=CARTESIAN_POINT('Ctrl Pts',(-20.2426723273843,-21.0219144506012,
3.31352568661436));
#151848=CARTESIAN_POINT('Ctrl Pts',(-20.3088136057118,-20.97030674261,3.31771032100697));
#151849=CARTESIAN_POINT('Ctrl Pts',(-20.374860740116,-20.9187724918035,
3.32188899909045));
#151850=CARTESIAN_POINT('Ctrl Pts',(-20.4384737424745,-20.8639162618918,
3.32606767717394));
#151851=CARTESIAN_POINT('Ctrl Pts',(-20.4993017308436,-20.8059983276909,
3.33024635525743));
#151852=CARTESIAN_POINT('Ctrl Pts',(-20.5612200171964,-20.7470422561363,
3.33449993314298));
#151853=CARTESIAN_POINT('Ctrl Pts',(-20.6202520574043,-20.6849138964936,
3.33875351102852));
#151854=CARTESIAN_POINT('Ctrl Pts',(-20.6760617089388,-20.6199317488056,
3.34300708891407));
#151855=CARTESIAN_POINT('Ctrl Pts',(-20.7307893814671,-20.5562094068616,
3.34717820289155));
#151856=CARTESIAN_POINT('Ctrl Pts',(-20.7824181813927,-20.4897433069906,
3.35134931686903));
#151857=CARTESIAN_POINT('Ctrl Pts',(-20.8306684931562,-20.4208707328441,
3.3555204308465));
#151858=CARTESIAN_POINT('Ctrl Pts',(-20.8789026140616,-20.352021269555,
3.3596901451664));
#151859=CARTESIAN_POINT('Ctrl Pts',(-20.923760234583,-20.2807673121879,
3.36385985948629));
#151860=CARTESIAN_POINT('Ctrl Pts',(-20.965003586852,-20.2074771983009,
3.36802957380619));
#151861=CARTESIAN_POINT('Ctrl Pts',(-21.0062454715054,-20.1341896923909,
3.37219913974974));
#151862=CARTESIAN_POINT('Ctrl Pts',(-21.0438731187515,-20.0588665753507,
3.3763687056933));
#151863=CARTESIAN_POINT('Ctrl Pts',(-21.0776941561667,-19.9819017925755,
3.38053827163685));
#151864=CARTESIAN_POINT('Ctrl Pts',(-21.1127042995432,-19.9022310229647,
3.38485443437633));
#151865=CARTESIAN_POINT('Ctrl Pts',(-21.1436349596428,-19.8208014806364,
3.38917059711581));
#151866=CARTESIAN_POINT('Ctrl Pts',(-21.1703273243944,-19.7380719867856,
3.39348675985529));
#151867=CARTESIAN_POINT('Ctrl Pts',(-21.1961501881654,-19.6580373975152,
3.39766232404647));
#151868=CARTESIAN_POINT('Ctrl Pts',(-21.2180065643708,-19.5767867151054,
3.40183788823765));
#151869=CARTESIAN_POINT('Ctrl Pts',(-21.2358041974883,-19.4947483371046,
3.40601345242883));
#151870=CARTESIAN_POINT('Ctrl Pts',(-21.2545007467516,-19.4085663956271,
3.41039991444246));
#151871=CARTESIAN_POINT('Ctrl Pts',(-21.2687176692139,-19.3215156705805,
3.41478637645609));
#151872=CARTESIAN_POINT('Ctrl Pts',(-21.2784095170101,-19.2340996450695,
3.41917283846971));
#151873=CARTESIAN_POINT('Ctrl Pts',(-21.2881013648063,-19.1466836195585,
3.42355930048334));
#151874=CARTESIAN_POINT('Ctrl Pts',(-21.293268179777,-19.0589028772671,
3.42794576249697));
#151875=CARTESIAN_POINT('Ctrl Pts',(-21.2939275539577,-18.9712592442245,
3.43233222451059));
#151876=CARTESIAN_POINT('Ctrl Pts',(-21.2939755504833,-18.9648795739236,
3.43265151959756));
#151877=CARTESIAN_POINT('Ctrl Pts',(-21.2939996986147,-18.958499723977,
3.43297081468453));
#151878=CARTESIAN_POINT('Ctrl Pts',(-21.2939999971965,-18.9521198086916,
3.4332901097715));
#151879=CARTESIAN_POINT('',(-21.2936055506457,-18.9523823947329,3.36670986511492));
#151880=CARTESIAN_POINT('Ctrl Pts',(-17.1746506047676,-20.9818836121461,
3.08342410085255));
#151881=CARTESIAN_POINT('Ctrl Pts',(-17.6886694217464,-21.3686027203593,
3.11541445624699));
#151882=CARTESIAN_POINT('Ctrl Pts',(-19.2309396521922,-21.8303673584937,
3.1897967472019));
#151883=CARTESIAN_POINT('Ctrl Pts',(-21.0089153287167,-20.6164715882702,
3.28422525530708));
#151884=CARTESIAN_POINT('Ctrl Pts',(-21.2903730986671,-19.3569817773889,
3.34666340801782));
#151885=CARTESIAN_POINT('Ctrl Pts',(-21.2898370719784,-18.9523866753572,
3.36670962516808));
#151886=CARTESIAN_POINT('Ctrl Pts',(-21.2939999715072,-18.9523819467093,
3.36670989022851));
#151887=CARTESIAN_POINT('Ctrl Pts',(-21.2940130064034,-18.8650154810554,
3.3710315430356));
#151888=CARTESIAN_POINT('Ctrl Pts',(-21.2895493128086,-18.777713537132,
3.37535319584269));
#151889=CARTESIAN_POINT('Ctrl Pts',(-21.2806546261691,-18.690944038544,
3.37967484864978));
#151890=CARTESIAN_POINT('Ctrl Pts',(-21.2713805337795,-18.6004733587877,
3.3841808429622));
#151891=CARTESIAN_POINT('Ctrl Pts',(-21.2572890869443,-18.5105820575898,
3.38868683727461));
#151892=CARTESIAN_POINT('Ctrl Pts',(-21.2384911684206,-18.4217887333304,
3.39319283158702));
#151893=CARTESIAN_POINT('Ctrl Pts',(-21.2204017935412,-18.3363422660907,
3.39752898296562));
#151894=CARTESIAN_POINT('Ctrl Pts',(-21.1979545494933,-18.2519128648075,
3.40186513434422));
#151895=CARTESIAN_POINT('Ctrl Pts',(-21.1712990035407,-18.1689459997295,
3.40620128572282));
#151896=CARTESIAN_POINT('Ctrl Pts',(-21.1446099328527,-18.0858747870536,
3.41054289068799));
#151897=CARTESIAN_POINT('Ctrl Pts',(-21.1137021554184,-18.0042701592823,
3.41488449565315));
#151898=CARTESIAN_POINT('Ctrl Pts',(-21.078773161122,-17.9245571437388,
3.41922610061831));
#151899=CARTESIAN_POINT('Ctrl Pts',(-21.043770395337,-17.8446757709914,
3.42357687523372));
#151900=CARTESIAN_POINT('Ctrl Pts',(-21.004729634837,-17.7666943545291,
3.42792764984912));
#151901=CARTESIAN_POINT('Ctrl Pts',(-20.9618940508663,-17.6910130460174,
3.43227842446453));
#151902=CARTESIAN_POINT('Ctrl Pts',(-20.9570751477607,-17.6824990756493,
3.4327678764426));
#151903=CARTESIAN_POINT('Ctrl Pts',(-20.9522082623988,-17.6740141830165,
3.43325732842066));
#151904=CARTESIAN_POINT('Ctrl Pts',(-20.9472937739975,-17.6655589131313,
3.43374678039873));
#151905=CARTESIAN_POINT('Ctrl Pts',(-20.9052767057114,-17.5932694654538,
3.43793141479117));
#151906=CARTESIAN_POINT('Ctrl Pts',(-20.8596361007271,-17.5229061642047,
3.44211604918361));
#151907=CARTESIAN_POINT('Ctrl Pts',(-20.8105736599317,-17.4548554395525,
3.44630068357605));
#151908=CARTESIAN_POINT('Ctrl Pts',(-20.7615810534482,-17.3869015766838,
3.45047936165939));
#151909=CARTESIAN_POINT('Ctrl Pts',(-20.7091765523541,-17.3212541220958,
3.45465803974272));
#151910=CARTESIAN_POINT('Ctrl Pts',(-20.6536069384428,-17.2582735752542,
3.45883671782606));
#151911=CARTESIAN_POINT('Ctrl Pts',(-20.5970412791291,-17.1941641473621,
3.46309029571165));
#151912=CARTESIAN_POINT('Ctrl Pts',(-20.5371961639065,-17.1328185931041,
3.46734387359723));
#151913=CARTESIAN_POINT('Ctrl Pts',(-20.4743771168501,-17.074584891095,
3.47159745148282));
#151914=CARTESIAN_POINT('Ctrl Pts',(-20.4127759396134,-17.0174801630436,
3.47576856546016));
#151915=CARTESIAN_POINT('Ctrl Pts',(-20.3483154653819,-16.9633680324697,
3.4799396794375));
#151916=CARTESIAN_POINT('Ctrl Pts',(-20.2813221318919,-16.9125407039714,
3.48411079341484));
#151917=CARTESIAN_POINT('Ctrl Pts',(-20.2143512786619,-16.8617304310739,
3.4882805077346));
#151918=CARTESIAN_POINT('Ctrl Pts',(-20.1448496203253,-16.8142030489947,
3.49245022205436));
#151919=CARTESIAN_POINT('Ctrl Pts',(-20.0731762130981,-16.7702101223371,
3.49661993637412));
#151920=CARTESIAN_POINT('Ctrl Pts',(-20.0015053563183,-16.7262187611366,
3.50078950231756));
#151921=CARTESIAN_POINT('Ctrl Pts',(-19.9276632968149,-16.6857618452166,
3.504959068261));
#151922=CARTESIAN_POINT('Ctrl Pts',(-19.8520364016659,-16.6490465474635,
3.50912863420444));
#151923=CARTESIAN_POINT('Ctrl Pts',(-19.7737505581549,-16.6110403851227,
3.51344479694408));
#151924=CARTESIAN_POINT('Ctrl Pts',(-19.6935525085947,-16.5770440773061,
3.51776095968372));
#151925=CARTESIAN_POINT('Ctrl Pts',(-19.6118947218444,-16.5472337208457,
3.52207712242337));
#151926=CARTESIAN_POINT('Ctrl Pts',(-19.5328969289333,-16.5183944336205,
3.52625268661444));
#151927=CARTESIAN_POINT('Ctrl Pts',(-19.4525335041398,-16.4934726654687,
3.53042825080552));
#151928=CARTESIAN_POINT('Ctrl Pts',(-19.3712290384547,-16.4725768508482,
3.5346038149966));
#151929=CARTESIAN_POINT('Ctrl Pts',(-19.2858180774516,-16.4506256382961,
3.53899027701053));
#151930=CARTESIAN_POINT('Ctrl Pts',(-19.1993690855434,-16.4331178853207,
3.54337673902446));
#151931=CARTESIAN_POINT('Ctrl Pts',(-19.112383460267,-16.4201180997139,
3.54776320103838));
#151932=CARTESIAN_POINT('Ctrl Pts',(-19.0253978349906,-16.4071183141071,
3.55214966305231));
#151933=CARTESIAN_POINT('Ctrl Pts',(-18.937876161197,-16.3986264761921,
3.55653612506623));
#151934=CARTESIAN_POINT('Ctrl Pts',(-18.8503205710795,-16.3946440363642,
3.56092258708016));
#151935=CARTESIAN_POINT('Ctrl Pts',(-18.7667935434872,-16.3908448344978,
3.56510722147276));
#151936=CARTESIAN_POINT('Ctrl Pts',(-18.6829247485327,-16.391135040087,
3.56929185586536));
#151937=CARTESIAN_POINT('Ctrl Pts',(-18.5991482896987,-16.3955542219267,
3.57347649025797));
#151938=CARTESIAN_POINT('Ctrl Pts',(-18.5154910762845,-16.3999671136081,
3.57765516834146));
#151939=CARTESIAN_POINT('Ctrl Pts',(-18.4319263933964,-16.4084972837709,
3.58183384642495));
#151940=CARTESIAN_POINT('Ctrl Pts',(-18.3488909423387,-16.4211323595045,
3.58601252450844));
#151941=CARTESIAN_POINT('Ctrl Pts',(-18.2643671404859,-16.4339939098917,
3.59026610239399));
#151942=CARTESIAN_POINT('Ctrl Pts',(-18.1803922116832,-16.4511089960901,
3.59451968027954));
#151943=CARTESIAN_POINT('Ctrl Pts',(-18.0974241252638,-16.4724090749271,
3.59877325816509));
#151944=CARTESIAN_POINT('Ctrl Pts',(-18.0160645371101,-16.4932962101692,
3.60294437214256));
#151945=CARTESIAN_POINT('Ctrl Pts',(-17.9356735666137,-16.5182073979463,
3.60711548612003));
#151946=CARTESIAN_POINT('Ctrl Pts',(-17.8566736061544,-16.5470263205885,
3.61128660009751));
#151947=CARTESIAN_POINT('Ctrl Pts',(-17.7777001548948,-16.575835572763,
3.6154563144174));
#151948=CARTESIAN_POINT('Ctrl Pts',(-17.7001172184807,-16.6085497980589,
3.6196260287373));
#151949=CARTESIAN_POINT('Ctrl Pts',(-17.6243306732527,-16.6450032541687,
3.6237957430572));
#151950=CARTESIAN_POINT('Ctrl Pts',(-17.5485468248353,-16.6814554131081,
3.62796530900076));
#151951=CARTESIAN_POINT('Ctrl Pts',(-17.4745596547067,-16.7216463381322,
3.63213487494432));
#151952=CARTESIAN_POINT('Ctrl Pts',(-17.4027524956497,-16.7653632944266,
3.63630444088788));
#151953=CARTESIAN_POINT('Ctrl Pts',(-17.3284206854457,-16.8106172849846,
3.64062060362735));
#151954=CARTESIAN_POINT('Ctrl Pts',(-17.2564254874565,-16.8596495964178,
3.64493676636683));
#151955=CARTESIAN_POINT('Ctrl Pts',(-17.1871598840616,-16.9121750918955,
3.64925292910631));
#151956=CARTESIAN_POINT('Ctrl Pts',(-17.1201506004283,-16.9629895748702,
3.65342849329749));
#151957=CARTESIAN_POINT('Ctrl Pts',(-17.0556961397385,-17.0170728169151,
3.65760405748868));
#151958=CARTESIAN_POINT('Ctrl Pts',(-16.9941175012612,-17.0741264977155,
3.66177962167986));
#151959=CARTESIAN_POINT('Ctrl Pts',(-16.92942867212,-17.1340618243228,3.66616608369348));
#151960=CARTESIAN_POINT('Ctrl Pts',(-16.8679142228486,-17.1972751310411,
3.67055254570711));
#151961=CARTESIAN_POINT('Ctrl Pts',(-16.8098997912682,-17.263379738734,
3.67493900772073));
#151962=CARTESIAN_POINT('Ctrl Pts',(-16.7518853596878,-17.3294843464269,
3.67932546973435));
#151963=CARTESIAN_POINT('Ctrl Pts',(-16.6973712458221,-17.3984797526768,
3.68371193174797));
#151964=CARTESIAN_POINT('Ctrl Pts',(-16.6466304638567,-17.4699445288448,
3.6880983937616));
#151965=CARTESIAN_POINT('Ctrl Pts',(-16.5982243404926,-17.538121104715,
3.69228302815506));
#151966=CARTESIAN_POINT('Ctrl Pts',(-16.5530717694469,-17.6087985715454,
3.69646766254852));
#151967=CARTESIAN_POINT('Ctrl Pts',(-16.5114409937959,-17.6816333348434,
3.70065229694198));
#151968=CARTESIAN_POINT('Ctrl Pts',(-16.4698694744012,-17.754364426871,
3.70483097502633));
#151969=CARTESIAN_POINT('Ctrl Pts',(-16.4318100196567,-17.8292463201214,
3.70900965311068));
#151970=CARTESIAN_POINT('Ctrl Pts',(-16.3974886040357,-17.905905120685,
3.71318833119504));
#151971=CARTESIAN_POINT('Ctrl Pts',(-16.3625520017104,-17.9839379751455,
3.71744190908037));
#151972=CARTESIAN_POINT('Ctrl Pts',(-16.3314890444374,-18.0638116724909,
3.7216954869657));
#151973=CARTESIAN_POINT('Ctrl Pts',(-16.3044899883695,-18.1451040318682,
3.72594906485104));
#151974=CARTESIAN_POINT('Ctrl Pts',(-16.2780143616845,-18.2248203802401,
3.73012017882942));
#151975=CARTESIAN_POINT('Ctrl Pts',(-16.2554466207297,-18.3059004177641,
3.73429129280781));
#151976=CARTESIAN_POINT('Ctrl Pts',(-16.2369175937363,-18.3879260187454,
3.73846240678619));
#151977=CARTESIAN_POINT('Ctrl Pts',(-16.2183947843369,-18.4699240952442,
3.742632121107));
#151978=CARTESIAN_POINT('Ctrl Pts',(-16.2039080986716,-18.5528666566984,
3.74680183542782));
#151979=CARTESIAN_POINT('Ctrl Pts',(-16.1935378668542,-18.6363227121694,
3.75097154974863));
#151980=CARTESIAN_POINT('Ctrl Pts',(-16.1831680040541,-18.7197757979158,
3.75514111569312));
#151981=CARTESIAN_POINT('Ctrl Pts',(-16.1769143597415,-18.8037418847219,
3.75931068163761));
#151982=CARTESIAN_POINT('Ctrl Pts',(-16.174805548368,-18.8877835010606,
3.76348024758209));
#151983=CARTESIAN_POINT('Ctrl Pts',(-16.1726225937887,-18.9747799169337,
3.7677964103205));
#151984=CARTESIAN_POINT('Ctrl Pts',(-16.1748813730051,-19.0618567451386,
3.77211257305891));
#151985=CARTESIAN_POINT('Ctrl Pts',(-16.1815548449752,-19.1485292105273,
3.77642873579733));
#151986=CARTESIAN_POINT('Ctrl Pts',(-16.1880109292993,-19.2323783294909,
3.78060429998945));
#151987=CARTESIAN_POINT('Ctrl Pts',(-16.1985983999138,-19.3158485639561,
3.78477986418157));
#151988=CARTESIAN_POINT('Ctrl Pts',(-16.2132401674605,-19.3985085292081,
3.78895542837369));
#151989=CARTESIAN_POINT('Ctrl Pts',(-16.2286214558734,-19.485343452771,
3.79334189038525));
#151990=CARTESIAN_POINT('Ctrl Pts',(-16.2484772384201,-19.5712835336828,
3.7977283523968));
#151991=CARTESIAN_POINT('Ctrl Pts',(-16.272658640717,-19.6558456599874,
3.80211481440836));
#151992=CARTESIAN_POINT('Ctrl Pts',(-16.2968400430139,-19.7404077862919,
3.80650127641991));
#151993=CARTESIAN_POINT('Ctrl Pts',(-16.3253468050044,-19.8235914337677,
3.81088773843147));
#151994=CARTESIAN_POINT('Ctrl Pts',(-16.3579723492966,-19.9049389293615,
3.81527420044303));
#151995=CARTESIAN_POINT('Ctrl Pts',(-16.3890953380463,-19.9825400007035,
3.81945864581547));
#151996=CARTESIAN_POINT('Ctrl Pts',(-16.4240819170418,-20.0587591592382,
3.82364309118791));
#151997=CARTESIAN_POINT('Ctrl Pts',(-16.4627883931821,-20.1331849292367,
3.82782753656036));
#151998=CARTESIAN_POINT('Ctrl Pts',(-16.5014420743038,-20.2075091836669,
3.83200627441578));
#151999=CARTESIAN_POINT('Ctrl Pts',(-16.5438053667044,-20.2800445024167,
3.8361850122712));
#152000=CARTESIAN_POINT('Ctrl Pts',(-16.5896861940544,-20.3503984774131,
3.84036375012661));
#152001=CARTESIAN_POINT('Ctrl Pts',(-16.6355124170914,-20.4206687217817,
3.84453751472581));
#152002=CARTESIAN_POINT('Ctrl Pts',(-16.6848476028014,-20.4887624000661,
3.84871127932502));
#152003=CARTESIAN_POINT('Ctrl Pts',(-16.7374540925185,-20.5543122165542,
3.85288504392422));
#152004=CARTESIAN_POINT('Ctrl Pts',(-16.7900243343999,-20.6198168667711,
3.85705593264376));
#152005=CARTESIAN_POINT('Ctrl Pts',(-16.8458611159082,-20.6827807792016,
3.86122682136329));
#152006=CARTESIAN_POINT('Ctrl Pts',(-16.9046845019153,-20.7428670549394,
3.86539771008283));
#152007=CARTESIAN_POINT('Ctrl Pts',(-16.9634896683972,-20.8029347199936,
3.86956730694181));
#152008=CARTESIAN_POINT('Ctrl Pts',(-17.0252792822203,-20.8601261886928,
3.87373690380078));
#152009=CARTESIAN_POINT('Ctrl Pts',(-17.0897351511593,-20.9141399305011,
3.87790650065976));
#152010=CARTESIAN_POINT('Ctrl Pts',(-17.117493244807,-20.9374010939616,
3.87970214878288));
#152011=CARTESIAN_POINT('Ctrl Pts',(-17.1457453692821,-20.9600733822345,
3.88149779690601));
#152012=CARTESIAN_POINT('Ctrl Pts',(-17.1744641402401,-20.9821349467765,
3.88329344502913));
#152013=CARTESIAN_POINT('Origin',(-18.734,-18.952,-1.76670989022851));
#152014=CARTESIAN_POINT('',(-17.1762220465436,-20.9798104602808,4.7499734600764));
#152015=CARTESIAN_POINT('',(-17.1735447294248,-20.9833104140832,4.68319929961578));
#152016=CARTESIAN_POINT('',(-17.1744641402401,-20.9821349467765,-1.76670989022851));
#152017=CARTESIAN_POINT('',(-21.2939990418858,-18.954214846262,4.23329008725046));
#152018=CARTESIAN_POINT('Ctrl Pts',(-21.2923872764654,-18.9542129983989,
4.2332901097715));
#152019=CARTESIAN_POINT('Ctrl Pts',(-21.2874612769029,-18.3551143891762,
4.26304769694121));
#152020=CARTESIAN_POINT('Ctrl Pts',(-20.7784813193811,-16.8950156348367,
4.3351972196714));
#152021=CARTESIAN_POINT('Ctrl Pts',(-18.3440265497682,-15.950131970293,
4.44973867796207));
#152022=CARTESIAN_POINT('Ctrl Pts',(-15.9988188107527,-17.6550517274584,
4.5769144846435));
#152023=CARTESIAN_POINT('Ctrl Pts',(-16.1279940901006,-19.9330437902871,
4.67699274534828));
#152024=CARTESIAN_POINT('Ctrl Pts',(-16.9304195254802,-20.7936897644837,
4.73467907049259));
#152025=CARTESIAN_POINT('Ctrl Pts',(-17.1762220465438,-20.9798104602809,
4.74997346007641));
#152026=CARTESIAN_POINT('Ctrl Pts',(-17.1744641402401,-20.9821349467765,
3.94993168147533));
#152027=CARTESIAN_POINT('Ctrl Pts',(-17.2408641401809,-21.033142975164,
3.95411195179436));
#152028=CARTESIAN_POINT('Ctrl Pts',(-17.309875151081,-21.0809712817735,
3.95829222211338));
#152029=CARTESIAN_POINT('Ctrl Pts',(-17.381159192972,-21.1253434498118,
3.96247249243241));
#152030=CARTESIAN_POINT('Ctrl Pts',(-17.4523585054123,-21.1696628763203,
3.9666477940095));
#152031=CARTESIAN_POINT('Ctrl Pts',(-17.5258250930132,-21.2105340841302,
3.9708230955866));
#152032=CARTESIAN_POINT('Ctrl Pts',(-17.6011898523106,-21.2477223632861,
3.9749983971637));
#152033=CARTESIAN_POINT('Ctrl Pts',(-17.6764914717807,-21.2848794864807,
3.97917020071568));
#152034=CARTESIAN_POINT('Ctrl Pts',(-17.7536876917253,-21.3183596094561,
3.98334200426766));
#152035=CARTESIAN_POINT('Ctrl Pts',(-17.8323836483386,-21.3479732791533,
3.98751380781964));
#152036=CARTESIAN_POINT('Ctrl Pts',(-17.911045866078,-21.3775742527489,
3.9916838228178));
#152037=CARTESIAN_POINT('Ctrl Pts',(-17.9912061137305,-21.4033119028792,
3.99585383781596));
#152038=CARTESIAN_POINT('Ctrl Pts',(-18.0724494594724,-21.4250448605571,
4.00002385281411));
#152039=CARTESIAN_POINT('Ctrl Pts',(-18.1536823453448,-21.4467750201731,
4.00419333093369));
#152040=CARTESIAN_POINT('Ctrl Pts',(-18.2359976077846,-21.4645013933133,
4.00836280905326));
#152041=CARTESIAN_POINT('Ctrl Pts',(-18.3189663842219,-21.4781328345465,
4.01253228717283));
#152042=CARTESIAN_POINT('Ctrl Pts',(-18.401949366933,-21.4917666098143,
4.01670247920854));
#152043=CARTESIAN_POINT('Ctrl Pts',(-18.4855856317187,-21.5013039876535,
4.02087267124424));
#152044=CARTESIAN_POINT('Ctrl Pts',(-18.5694387459347,-21.5067053829474,
4.02504286327995));
#152045=CARTESIAN_POINT('Ctrl Pts',(-18.6533842887412,-21.5121127320256,
4.02921765198419));
#152046=CARTESIAN_POINT('Ctrl Pts',(-18.7375466982335,-21.5133749703138,
4.03339244068844));
#152047=CARTESIAN_POINT('Ctrl Pts',(-18.8214876223156,-21.51050462496,4.03756722939268));
#152048=CARTESIAN_POINT('Ctrl Pts',(-18.9054811188542,-21.5076324819001,
4.04174463277981));
#152049=CARTESIAN_POINT('Ctrl Pts',(-18.9892523957867,-21.5006226419762,
4.04592203616693));
#152050=CARTESIAN_POINT('Ctrl Pts',(-19.0723687017023,-21.4895394818029,
4.05009943955406));
#152051=CARTESIAN_POINT('Ctrl Pts',(-19.155621576138,-21.4784381108733,
4.05428370683862));
#152052=CARTESIAN_POINT('Ctrl Pts',(-19.2382168797992,-21.46325014424,4.05846797412318));
#152053=CARTESIAN_POINT('Ctrl Pts',(-19.3197329580376,-21.4440908695047,
4.06265224140774));
#152054=CARTESIAN_POINT('Ctrl Pts',(-19.3558324065943,-21.4356061721586,
4.06450524691108));
#152055=CARTESIAN_POINT('Ctrl Pts',(-19.3917204150806,-21.4263432877792,
4.06635825241442));
#152056=CARTESIAN_POINT('Ctrl Pts',(-19.4273615317731,-21.4163152773656,
4.06821125791777));
#152057=CARTESIAN_POINT('Ctrl Pts',(-19.5078497129731,-21.3936690643915,
4.07239589231081));
#152058=CARTESIAN_POINT('Ctrl Pts',(-19.5873770243866,-21.3670332665356,
4.07658052670385));
#152059=CARTESIAN_POINT('Ctrl Pts',(-19.6655189252301,-21.336506760724,
4.08076516109689));
#152060=CARTESIAN_POINT('Ctrl Pts',(-19.7435496007498,-21.3060237056149,
4.08494383918084));
#152061=CARTESIAN_POINT('Ctrl Pts',(-19.820198357802,-21.2716611086064,
4.08912251726478));
#152062=CARTESIAN_POINT('Ctrl Pts',(-19.8950545149195,-21.2335679725542,
4.09330119534872));
#152063=CARTESIAN_POINT('Ctrl Pts',(-19.9712524148552,-21.1947920444153,
4.09755477323416));
#152064=CARTESIAN_POINT('Ctrl Pts',(-20.0455923539257,-21.152150652534,
4.10180835111959));
#152065=CARTESIAN_POINT('Ctrl Pts',(-20.1176611149874,-21.1058528080795,
4.10606192900503));
#152066=CARTESIAN_POINT('Ctrl Pts',(-20.1883326824852,-21.0604525376826,
4.11023304298298));
#152067=CARTESIAN_POINT('Ctrl Pts',(-20.2568199436825,-21.0115365845692,
4.11440415696092));
#152068=CARTESIAN_POINT('Ctrl Pts',(-20.3227584711504,-20.9593481313285,
4.11857527093886));
#152069=CARTESIAN_POINT('Ctrl Pts',(-20.3886748723086,-20.9071771904272,
4.12274498525923));
#152070=CARTESIAN_POINT('Ctrl Pts',(-20.4520438778608,-20.8517362155432,
4.1269146995796));
#152071=CARTESIAN_POINT('Ctrl Pts',(-20.512532273786,-20.7933101181229,
4.13108441389997));
#152072=CARTESIAN_POINT('Ctrl Pts',(-20.5730185172742,-20.7348860997541,
4.13525397984399));
#152073=CARTESIAN_POINT('Ctrl Pts',(-20.6306240246485,-20.6734774902644,
4.13942354578802));
#152074=CARTESIAN_POINT('Ctrl Pts',(-20.6850517529254,-20.6094067266084,
4.14359311173205));
#152075=CARTESIAN_POINT('Ctrl Pts',(-20.7413930929849,-20.5430833139418,
4.14790927447098));
#152076=CARTESIAN_POINT('Ctrl Pts',(-20.7943286933419,-20.47390746331,4.1522254372099));
#152077=CARTESIAN_POINT('Ctrl Pts',(-20.8435751066795,-20.4022733774286,
4.15654159994883));
#152078=CARTESIAN_POINT('Ctrl Pts',(-20.8912173232822,-20.3329727643606,
4.16071716414051));
#152079=CARTESIAN_POINT('Ctrl Pts',(-20.9354068051746,-20.261372036261,
4.16489272833218));
#152080=CARTESIAN_POINT('Ctrl Pts',(-20.9759325838393,-20.1878552866415,
4.16906829252385));
#152081=CARTESIAN_POINT('Ctrl Pts',(-21.0185052232437,-20.1106253807678,
4.17345475453641));
#152082=CARTESIAN_POINT('Ctrl Pts',(-21.0570340704736,-20.0312813353546,
4.17784121654897));
#152083=CARTESIAN_POINT('Ctrl Pts',(-21.0913315250628,-19.9502925828359,
4.18222767856152));
#152084=CARTESIAN_POINT('Ctrl Pts',(-21.125628979652,-19.8693038303172,
4.18661414057408));
#152085=CARTESIAN_POINT('Ctrl Pts',(-21.1556949146933,-19.7866709419479,
4.19100060258664));
#152086=CARTESIAN_POINT('Ctrl Pts',(-21.1814026084241,-19.7028797988221,
4.19538706459919));
#152087=CARTESIAN_POINT('Ctrl Pts',(-21.2113658472603,-19.6052182170354,
4.20049964335886));
#152088=CARTESIAN_POINT('Ctrl Pts',(-21.235501378659,-19.5056900725396,
4.20561222211854));
#152089=CARTESIAN_POINT('Ctrl Pts',(-21.253614967081,-19.4049242957285,
4.2107248008782));
#152090=CARTESIAN_POINT('Ctrl Pts',(-21.2714816855059,-19.3055318551366,
4.21576770033001));
#152091=CARTESIAN_POINT('Ctrl Pts',(-21.283489454374,-19.2049352741372,
4.22081059978182));
#152092=CARTESIAN_POINT('Ctrl Pts',(-21.2894978367355,-19.1037590407195,
4.22585349923363));
#152093=CARTESIAN_POINT('Ctrl Pts',(-21.2924512874039,-19.0540253526423,
4.22833236190591));
#152094=CARTESIAN_POINT('Ctrl Pts',(-21.2939558375883,-19.0041519285412,
4.23081122457819));
#152095=CARTESIAN_POINT('Ctrl Pts',(-21.2939990418858,-18.954214846262,
4.23329008725046));
#152096=CARTESIAN_POINT('',(-21.2939989159607,-18.9496440968075,4.16670989022851));
#152097=CARTESIAN_POINT('Ctrl Pts',(-17.1744641402401,-20.9821349467765,
3.88329344502913));
#152098=CARTESIAN_POINT('Ctrl Pts',(-17.2411550934206,-21.033366483464,
3.88746331306014));
#152099=CARTESIAN_POINT('Ctrl Pts',(-17.3103644275838,-21.0813016244736,
3.89163318109116));
#152100=CARTESIAN_POINT('Ctrl Pts',(-17.381727523325,-21.1256971152457,
3.89580304912217));
#152101=CARTESIAN_POINT('Ctrl Pts',(-17.4531658161136,-21.1701393866372,
3.89997731104559));
#152102=CARTESIAN_POINT('Ctrl Pts',(-17.5267620105389,-21.2110343169657,
3.904151572969));
#152103=CARTESIAN_POINT('Ctrl Pts',(-17.6021247933809,-21.2481834675481,
3.90832583489242));
#152104=CARTESIAN_POINT('Ctrl Pts',(-17.6775291402241,-21.2853531065901,
3.91250239900029));
#152105=CARTESIAN_POINT('Ctrl Pts',(-17.7547015931812,-21.3187726695461,
3.91667896310817));
#152106=CARTESIAN_POINT('Ctrl Pts',(-17.8332308997776,-21.3482919329841,
3.92085552721604));
#152107=CARTESIAN_POINT('Ctrl Pts',(-17.9118958332387,-21.3778621787281,
3.92503930460925));
#152108=CARTESIAN_POINT('Ctrl Pts',(-17.9919218622461,-21.4035185308936,
3.92922308200245));
#152109=CARTESIAN_POINT('Ctrl Pts',(-18.0728828643972,-21.4251607576161,
3.93340685939566));
#152110=CARTESIAN_POINT('Ctrl Pts',(-18.1312147045753,-21.440753831772,
3.93642124197193));
#152111=CARTESIAN_POINT('Ctrl Pts',(-18.1900316123881,-21.4542641966054,
3.9394356245482));
#152112=CARTESIAN_POINT('Ctrl Pts',(-18.249172131343,-21.4656710082613,
3.94245000712447));
#152113=CARTESIAN_POINT('Ctrl Pts',(-18.3312723437007,-21.4815062034173,
3.94663464151747));
#152114=CARTESIAN_POINT('Ctrl Pts',(-18.4143019582716,-21.4933443659487,
3.95081927591047));
#152115=CARTESIAN_POINT('Ctrl Pts',(-18.4978371529755,-21.5010835823263,
3.95500391030347));
#152116=CARTESIAN_POINT('Ctrl Pts',(-18.5812534456693,-21.5088117828872,
3.95918258838737));
#152117=CARTESIAN_POINT('Ctrl Pts',(-18.6651734349298,-21.5124525840588,
3.96336126647127));
#152118=CARTESIAN_POINT('Ctrl Pts',(-18.7491632186831,-21.511955092731,
3.96753994455517));
#152119=CARTESIAN_POINT('Ctrl Pts',(-18.8346584589489,-21.5114486842286,
3.97179352244062));
#152120=CARTESIAN_POINT('Ctrl Pts',(-18.9202255470372,-21.5066540748902,
3.97604710032607));
#152121=CARTESIAN_POINT('Ctrl Pts',(-19.0054014154827,-21.4975728769128,
3.98030067821151));
#152122=CARTESIAN_POINT('Ctrl Pts',(-19.0889259835101,-21.4886677356788,
3.98447179218942));
#152123=CARTESIAN_POINT('Ctrl Pts',(-19.1720738871336,-21.4756407813847,
3.98864290616732));
#152124=CARTESIAN_POINT('Ctrl Pts',(-19.254410355074,-21.4585460423323,
3.99281402014522));
#152125=CARTESIAN_POINT('Ctrl Pts',(-19.3367191942173,-21.4414570395848,
3.99698373446554));
#152126=CARTESIAN_POINT('Ctrl Pts',(-19.4182166883876,-21.4203030563999,
4.00115344878586));
#152127=CARTESIAN_POINT('Ctrl Pts',(-19.4984772632651,-21.3951894142597,
4.00532316310618));
#152128=CARTESIAN_POINT('Ctrl Pts',(-19.5787349821269,-21.3700766657707,
4.00949272905017));
#152129=CARTESIAN_POINT('Ctrl Pts',(-19.6577554304214,-21.3410046766651,
4.01366229499415));
#152130=CARTESIAN_POINT('Ctrl Pts',(-19.7351285466055,-21.3081285264543,
4.01783186093814));
#152131=CARTESIAN_POINT('Ctrl Pts',(-19.8152220061068,-21.2740964913582,
4.02214802367712));
#152132=CARTESIAN_POINT('Ctrl Pts',(-19.8935496523619,-21.235988015554,
4.0264641864161));
#152133=CARTESIAN_POINT('Ctrl Pts',(-19.9696814081004,-21.1940284248142,
4.03078034915508));
#152134=CARTESIAN_POINT('Ctrl Pts',(-20.0433331799013,-21.1534356633306,
4.0349559133467));
#152135=CARTESIAN_POINT('Ctrl Pts',(-20.1149295504521,-21.1092391216319,
4.03913147753832));
#152136=CARTESIAN_POINT('Ctrl Pts',(-20.1841097633276,-21.0616875774157,
4.04330704172994));
#152137=CARTESIAN_POINT('Ctrl Pts',(-20.2567841042981,-21.0117343177421,
4.0476935037426));
#152138=CARTESIAN_POINT('Ctrl Pts',(-20.3267913293727,-20.9580785813376,
4.05207996575526));
#152139=CARTESIAN_POINT('Ctrl Pts',(-20.3937533178436,-20.9010559057932,
4.05646642776792));
#152140=CARTESIAN_POINT('Ctrl Pts',(-20.4607153063145,-20.8440332302488,
4.06085288978057));
#152141=CARTESIAN_POINT('Ctrl Pts',(-20.5246316886731,-20.7836440693277,
4.06523935179323));
#152142=CARTESIAN_POINT('Ctrl Pts',(-20.5851713910718,-20.7202659530956,
4.06962581380589));
#152143=CARTESIAN_POINT('Ctrl Pts',(-20.6421808499863,-20.66058359639,4.07375648865202));
#152144=CARTESIAN_POINT('Ctrl Pts',(-20.6964202744403,-20.5980163329693,
4.07788716349815));
#152145=CARTESIAN_POINT('Ctrl Pts',(-20.747578131795,-20.5328551822216,
4.08201783834428));
#152146=CARTESIAN_POINT('Ctrl Pts',(-20.7986699217385,-20.467778183328,
4.08614317866296));
#152147=CARTESIAN_POINT('Ctrl Pts',(-20.8466877493678,-20.4001143092104,
4.09026851898165));
#152148=CARTESIAN_POINT('Ctrl Pts',(-20.8913569516645,-20.3301911997632,
4.09439385930034));
#152149=CARTESIAN_POINT('Ctrl Pts',(-20.9359826817961,-20.2603361396387,
4.09851518482882));
#152150=CARTESIAN_POINT('Ctrl Pts',(-20.9772659998208,-20.188226602647,
4.10263651035731));
#152151=CARTESIAN_POINT('Ctrl Pts',(-21.0149735460513,-20.1142218730579,
4.10675783588579));
#152152=CARTESIAN_POINT('Ctrl Pts',(-21.0526563884391,-20.0402656271644,
4.11087646135587));
#152153=CARTESIAN_POINT('Ctrl Pts',(-21.0867678956212,-19.9644170734847,
4.11499508682595));
#152154=CARTESIAN_POINT('Ctrl Pts',(-21.1171197545789,-19.8870616211436,
4.11911371229603));
#152155=CARTESIAN_POINT('Ctrl Pts',(-21.1474714047475,-19.8097067009274,
4.12323230943426));
#152156=CARTESIAN_POINT('Ctrl Pts',(-21.1740632676919,-19.730845335542,
4.12735090657249));
#152157=CARTESIAN_POINT('Ctrl Pts',(-21.1967549321189,-19.6508834983916,
4.13146950371072));
#152158=CARTESIAN_POINT('Ctrl Pts',(-21.2194452848828,-19.5709262833344,
4.13558786277862));
#152159=CARTESIAN_POINT('Ctrl Pts',(-21.238235765403,-19.4898691801177,
4.13970622184653));
#152160=CARTESIAN_POINT('Ctrl Pts',(-21.2530362470693,-19.4081319830388,
4.14382458091443));
#152161=CARTESIAN_POINT('Ctrl Pts',(-21.2678499327185,-19.3263218655936,
4.14794661410211));
#152162=CARTESIAN_POINT('Ctrl Pts',(-21.2786664327327,-19.2438309098082,
4.15206864728979));
#152163=CARTESIAN_POINT('Ctrl Pts',(-21.2854471635996,-19.1610869947161,
4.15619068047747));
#152164=CARTESIAN_POINT('Ctrl Pts',(-21.2912151852698,-19.090700969273,
4.15969708372782));
#152165=CARTESIAN_POINT('Ctrl Pts',(-21.2940637843831,-19.0201321760509,
4.16320348697816));
#152166=CARTESIAN_POINT('Ctrl Pts',(-21.2939989159607,-18.9496440968075,
4.16670989022851));
#152167=CARTESIAN_POINT('Ctrl Pts',(-21.2939116738757,-18.9496434105868,
4.1667099283594));
#152168=CARTESIAN_POINT('Ctrl Pts',(-21.2957663705073,-18.7480072535544,
4.17674049240205));
#152169=CARTESIAN_POINT('Ctrl Pts',(-21.1817725642886,-17.6962740222633,
4.22916299200517));
#152170=CARTESIAN_POINT('Ctrl Pts',(-19.7309870059684,-16.0937999128286,
4.32397742716877));
#152171=CARTESIAN_POINT('Ctrl Pts',(-16.8703562036358,-16.5666022074633,
4.4511532338502));
#152172=CARTESIAN_POINT('Ctrl Pts',(-15.7867861847936,-19.0722717083388,
4.57089385799921));
#152173=CARTESIAN_POINT('Ctrl Pts',(-16.6213792802803,-20.5504282248243,
4.64824254658773));
#152174=CARTESIAN_POINT('Ctrl Pts',(-17.1735447294247,-20.9833104140831,
4.68319929961578));
#152175=CARTESIAN_POINT('Origin',(-18.734,-18.952,-1.76670989022851));
#152176=CARTESIAN_POINT('',(-17.1744641402401,-20.9821349467765,5.54983330998614));
#152177=CARTESIAN_POINT('',(-17.1744641402401,-20.9821349467765,5.48336964453106));
#152178=CARTESIAN_POINT('',(-17.1744641402401,-20.9821349467765,-1.76670989022851));
#152179=CARTESIAN_POINT('',(-21.2938494922829,-18.9508032548851,5.03329016024732));
#152180=CARTESIAN_POINT('Ctrl Pts',(-21.2939997202205,-18.9508031412445,
5.03329016239894));
#152181=CARTESIAN_POINT('Ctrl Pts',(-21.2939564765218,-18.8583078019835,
5.03786858507833));
#152182=CARTESIAN_POINT('Ctrl Pts',(-21.2888961385929,-18.7659792628466,
5.04244700775773));
#152183=CARTESIAN_POINT('Ctrl Pts',(-21.2788976615006,-18.6743385289801,
5.04702543043713));
#152184=CARTESIAN_POINT('Ctrl Pts',(-21.2688681118673,-18.5824130006966,
5.05161808160601));
#152185=CARTESIAN_POINT('Ctrl Pts',(-21.2538698091559,-18.4911798450256,
5.05621073277489));
#152186=CARTESIAN_POINT('Ctrl Pts',(-21.2340326305246,-18.40114897993,5.06080338394377));
#152187=CARTESIAN_POINT('Ctrl Pts',(-21.2141037578095,-18.3107019620212,
5.06541726388461));
#152188=CARTESIAN_POINT('Ctrl Pts',(-21.1892913049386,-18.2214686542029,
5.07003114382545));
#152189=CARTESIAN_POINT('Ctrl Pts',(-21.1597755903596,-18.1339457321084,
5.0746450237663));
#152190=CARTESIAN_POINT('Ctrl Pts',(-21.1363775884172,-18.0645636578345,
5.07830258630061));
#152191=CARTESIAN_POINT('Ctrl Pts',(-21.1100249393917,-17.9962560714796,
5.08196014883493));
#152192=CARTESIAN_POINT('Ctrl Pts',(-21.0808281256644,-17.9292596866307,
5.08561771136924));
#152193=CARTESIAN_POINT('Ctrl Pts',(-21.0474239145964,-17.8526088095457,
5.08980234576229));
#152194=CARTESIAN_POINT('Ctrl Pts',(-21.0101982941979,-17.7774535557438,
5.09398698015533));
#152195=CARTESIAN_POINT('Ctrl Pts',(-20.9693070771845,-17.7042010295369,
5.09817161454838));
#152196=CARTESIAN_POINT('Ctrl Pts',(-20.9284740637572,-17.6310527692342,
5.10235029263232));
#152197=CARTESIAN_POINT('Ctrl Pts',(-20.8839860396696,-17.5598022552459,
5.10652897071627));
#152198=CARTESIAN_POINT('Ctrl Pts',(-20.8360465870686,-17.4908360304904,
5.11070764880022));
#152199=CARTESIAN_POINT('Ctrl Pts',(-20.7872478542333,-17.4206336357213,
5.11496122668565));
#152200=CARTESIAN_POINT('Ctrl Pts',(-20.7348729347517,-17.352798669429,
5.11921480457109));
#152201=CARTESIAN_POINT('Ctrl Pts',(-20.6791852047646,-17.2877120083456,
5.12346838245653));
#152202=CARTESIAN_POINT('Ctrl Pts',(-20.6245770900889,-17.2238871791935,
5.12763949643448));
#152203=CARTESIAN_POINT('Ctrl Pts',(-20.5667837820755,-17.1627054093254,
5.13181061041243));
#152204=CARTESIAN_POINT('Ctrl Pts',(-20.5060958601737,-17.1044945839443,
5.13598172439038));
#152205=CARTESIAN_POINT('Ctrl Pts',(-20.4454283026902,-17.0463032917677,
5.14015143871076));
#152206=CARTESIAN_POINT('Ctrl Pts',(-20.3818683920876,-16.9910812823424,
5.14432115303113));
#152207=CARTESIAN_POINT('Ctrl Pts',(-20.3157437934271,-16.9391198316952,
5.1484908673515));
#152208=CARTESIAN_POINT('Ctrl Pts',(-20.2496215477636,-16.8871602300594,
5.15266043329554));
#152209=CARTESIAN_POINT('Ctrl Pts',(-20.1809351577375,-16.8384612400848,
5.15682999923958));
#152210=CARTESIAN_POINT('Ctrl Pts',(-20.1100445342429,-16.7932731901002,
5.16099956518362));
#152211=CARTESIAN_POINT('Ctrl Pts',(-20.0366614838791,-16.7464963840235,
5.16531572792255));
#152212=CARTESIAN_POINT('Ctrl Pts',(-19.9609167591474,-16.703482284346,
5.16963189066146));
#152213=CARTESIAN_POINT('Ctrl Pts',(-19.8832395142303,-16.6644579700185,
5.17394805340038));
#152214=CARTESIAN_POINT('Ctrl Pts',(-19.8080925973962,-16.6267048686257,
5.17812361759207));
#152215=CARTESIAN_POINT('Ctrl Pts',(-19.731137580502,-16.5926857570977,
5.18229918178375));
#152216=CARTESIAN_POINT('Ctrl Pts',(-19.6527837251095,-16.5625572895602,
5.18647474597543));
#152217=CARTESIAN_POINT('Ctrl Pts',(-19.5704724027498,-16.530907104751,
5.19086120798797));
#152218=CARTESIAN_POINT('Ctrl Pts',(-19.4866177726054,-16.5035511069691,
5.19524767000051));
#152219=CARTESIAN_POINT('Ctrl Pts',(-19.4017104542219,-16.4806111699446,
5.19963413201305));
#152220=CARTESIAN_POINT('Ctrl Pts',(-19.3168031358384,-16.45767123292,5.20402059402559));
#152221=CARTESIAN_POINT('Ctrl Pts',(-19.2308437124363,-16.439147404523,
5.20840705603813));
#152222=CARTESIAN_POINT('Ctrl Pts',(-19.1443308019265,-16.4250990060965,
5.21279351805067));
#152223=CARTESIAN_POINT('Ctrl Pts',(-19.0617984786721,-16.4116969953064,
5.21697815244371));
#152224=CARTESIAN_POINT('Ctrl Pts',(-18.9784552815195,-16.4023177375285,
5.22116278683676));
#152225=CARTESIAN_POINT('Ctrl Pts',(-18.894727859237,-16.3970505767697,
5.22534742122981));
#152226=CARTESIAN_POINT('Ctrl Pts',(-18.8111196125767,-16.3917909131622,
5.22952609931376));
#152227=CARTESIAN_POINT('Ctrl Pts',(-18.7271286822944,-16.3906317491884,
5.2337047773977));
#152228=CARTESIAN_POINT('Ctrl Pts',(-18.6431902849674,-16.3936111328307,
5.23788345548164));
#152229=CARTESIAN_POINT('Ctrl Pts',(-18.5577473521939,-16.3966439197836,
5.24213703336708));
#152230=CARTESIAN_POINT('Ctrl Pts',(-18.4723593301118,-16.4039651578947,
5.24639061125252));
#152231=CARTESIAN_POINT('Ctrl Pts',(-18.3874890362874,-16.4155595508613,
5.25064418913795));
#152232=CARTESIAN_POINT('Ctrl Pts',(-18.3042641187195,-16.4269291638956,
5.2548153031159));
#152233=CARTESIAN_POINT('Ctrl Pts',(-18.2215375109946,-16.44240765832,5.25898641709385));
#152234=CARTESIAN_POINT('Ctrl Pts',(-18.1397421978239,-16.4619281808444,
5.26315753107181));
#152235=CARTESIAN_POINT('Ctrl Pts',(-18.0579743318605,-16.4814421530689,
5.26732724539218));
#152236=CARTESIAN_POINT('Ctrl Pts',(-17.9771375869061,-16.5049953529781,
5.27149695971255));
#152237=CARTESIAN_POINT('Ctrl Pts',(-17.8976542388869,-16.5324699282984,
5.27566667403293));
#152238=CARTESIAN_POINT('Ctrl Pts',(-17.8181737192263,-16.5599435259556,
5.27983623997697));
#152239=CARTESIAN_POINT('Ctrl Pts',(-17.7400469352591,-16.5913380704868,
5.28400580592101));
#152240=CARTESIAN_POINT('Ctrl Pts',(-17.6636791864353,-16.6264864317639,
5.28817537186506));
#152241=CARTESIAN_POINT('Ctrl Pts',(-17.5846264417726,-16.6628705660634,
5.29249153460398));
#152242=CARTESIAN_POINT('Ctrl Pts',(-17.5074592081877,-16.7032771763716,
5.2968076973429));
#152243=CARTESIAN_POINT('Ctrl Pts',(-17.4326007161618,-16.7474683254656,
5.30112386008182));
#152244=CARTESIAN_POINT('Ctrl Pts',(-17.36018073164,-16.7902199525259,5.3052994242735));
#152245=CARTESIAN_POINT('Ctrl Pts',(-17.2899217514086,-16.8365130434918,
5.30947498846518));
#152246=CARTESIAN_POINT('Ctrl Pts',(-17.2221770223174,-16.886088268064,
5.31365055265686));
#152247=CARTESIAN_POINT('Ctrl Pts',(-17.1510106680076,-16.9381674193753,
5.3180370146694));
#152248=CARTESIAN_POINT('Ctrl Pts',(-17.0826196821852,-16.9938686102921,
5.32242347668194));
#152249=CARTESIAN_POINT('Ctrl Pts',(-17.0173721044249,-17.0528452753571,
5.32680993869448));
#152250=CARTESIAN_POINT('Ctrl Pts',(-16.9521245266647,-17.1118219404221,
5.33119640070702));
#152251=CARTESIAN_POINT('Ctrl Pts',(-16.890020712904,-17.1740736151505,
5.33558286271956));
#152252=CARTESIAN_POINT('Ctrl Pts',(-16.8313804354228,-17.239213150305,
5.3399693247321));
#152253=CARTESIAN_POINT('Ctrl Pts',(-16.7754382840343,-17.3013555188871,
5.34415395912515));
#152254=CARTESIAN_POINT('Ctrl Pts',(-16.7224397206528,-17.3663571440021,
5.34833859351819));
#152255=CARTESIAN_POINT('Ctrl Pts',(-16.6726908063355,-17.4339076417707,
5.35252322791124));
#152256=CARTESIAN_POINT('Ctrl Pts',(-16.6230127034401,-17.5013619897667,
5.35670190599519));
#152257=CARTESIAN_POINT('Ctrl Pts',(-16.576575332432,-17.5713576368075,
5.36088058407914));
#152258=CARTESIAN_POINT('Ctrl Pts',(-16.533646260122,-17.6435492292772,
5.36505926216308));
#152259=CARTESIAN_POINT('Ctrl Pts',(-16.4899477150435,-17.7170348041588,
5.36931284004852));
#152260=CARTESIAN_POINT('Ctrl Pts',(-16.4498848008428,-17.7927954651137,
5.37356641793395));
#152261=CARTESIAN_POINT('Ctrl Pts',(-16.4136951701205,-17.8704337762126,
5.37781999581938));
#152262=CARTESIAN_POINT('Ctrl Pts',(-16.378207146008,-17.9465669171521,
5.38199110979734));
#152263=CARTESIAN_POINT('Ctrl Pts',(-16.3464437665668,-18.0245051179384,
5.38616222377529));
#152264=CARTESIAN_POINT('Ctrl Pts',(-16.3185831851716,-18.1038481205324,
5.39033333775324));
#152265=CARTESIAN_POINT('Ctrl Pts',(-16.2907319526636,-18.1831644988157,
5.39450305207362));
#152266=CARTESIAN_POINT('Ctrl Pts',(-16.2667810695588,-18.2638843090191,
5.39867276639399));
#152267=CARTESIAN_POINT('Ctrl Pts',(-16.2468600106956,-18.3455886927151,
5.40284248071436));
#152268=CARTESIAN_POINT('Ctrl Pts',(-16.2269396607092,-18.4272901690185,
5.40701204665841));
#152269=CARTESIAN_POINT('Ctrl Pts',(-16.2110489579957,-18.5099757020134,
5.41118161260245));
#152270=CARTESIAN_POINT('Ctrl Pts',(-16.1992667534716,-18.5932140346339,
5.4153511785465));
#152271=CARTESIAN_POINT('Ctrl Pts',(-16.1870703011713,-18.6793789243438,
5.41966734128542));
#152272=CARTESIAN_POINT('Ctrl Pts',(-16.1792767060087,-18.7661356875971,
5.42398350402433));
#152273=CARTESIAN_POINT('Ctrl Pts',(-16.1759149870658,-18.8529996636308,
5.42829966676326));
#152274=CARTESIAN_POINT('Ctrl Pts',(-16.1726627757638,-18.9370340547817,
5.43247523095494));
#152275=CARTESIAN_POINT('Ctrl Pts',(-16.1735580857934,-19.0211683105535,
5.43665079514662));
#152276=CARTESIAN_POINT('Ctrl Pts',(-16.1785740672325,-19.1049650356758,
5.4408263593383));
#152277=CARTESIAN_POINT('Ctrl Pts',(-16.1838433939698,-19.1929941341762,
5.44521282135084));
#152278=CARTESIAN_POINT('Ctrl Pts',(-16.1936605371381,-19.2806501283313,
5.44959928336338));
#152279=CARTESIAN_POINT('Ctrl Pts',(-16.2079333028747,-19.3674359657934,
5.45398574537592));
#152280=CARTESIAN_POINT('Ctrl Pts',(-16.2222060686114,-19.4542218032555,
5.45837220738846));
#152281=CARTESIAN_POINT('Ctrl Pts',(-16.2409342590202,-19.5401369333207,
5.462758669401));
#152282=CARTESIAN_POINT('Ctrl Pts',(-16.2639654295305,-19.6247029215675,
5.46714513141354));
#152283=CARTESIAN_POINT('Ctrl Pts',(-16.2859330287312,-19.7053636823823,
5.47132902816154));
#152284=CARTESIAN_POINT('Ctrl Pts',(-16.3118967078507,-19.7850973400462,
5.47551292490953));
#152285=CARTESIAN_POINT('Ctrl Pts',(-16.3417612031338,-19.8634787648475,
5.47969682165753));
#152286=CARTESIAN_POINT('Ctrl Pts',(-16.3715858706222,-19.9417556588589,
5.48387513869027));
#152287=CARTESIAN_POINT('Ctrl Pts',(-16.4053008633503,-20.018683474586,
5.488053455723));
#152288=CARTESIAN_POINT('Ctrl Pts',(-16.4427606711044,-20.0938504007627,
5.49223177275574));
#152289=CARTESIAN_POINT('Ctrl Pts',(-16.4801817643412,-20.1689396423106,
5.49640577151947));
#152290=CARTESIAN_POINT('Ctrl Pts',(-16.5213397815898,-20.242271199406,
5.5005797702832));
#152291=CARTESIAN_POINT('Ctrl Pts',(-16.5660409635171,-20.31345275942,5.50475376904693));
#152292=CARTESIAN_POINT('Ctrl Pts',(-16.6107117825595,-20.384585969985,
5.50892493265869));
#152293=CARTESIAN_POINT('Ctrl Pts',(-16.6589207423439,-20.4535716954381,
5.51309609627045));
#152294=CARTESIAN_POINT('Ctrl Pts',(-16.7104285670038,-20.5200429380478,
5.51726725988221));
#152295=CARTESIAN_POINT('Ctrl Pts',(-16.7619153763091,-20.5864870601814,
5.52143672164609));
#152296=CARTESIAN_POINT('Ctrl Pts',(-16.8166980925858,-20.6504183762542,
5.52560618340997));
#152297=CARTESIAN_POINT('Ctrl Pts',(-16.8744954343627,-20.7115007162187,
5.52977564517385));
#152298=CARTESIAN_POINT('Ctrl Pts',(-16.9323025068466,-20.7725933399494,
5.53394580890445));
#152299=CARTESIAN_POINT('Ctrl Pts',(-16.9931249059,-20.8308356918097,5.53811597263505));
#152300=CARTESIAN_POINT('Ctrl Pts',(-17.0566432414223,-20.8859271714451,
5.54228613636565));
#152301=CARTESIAN_POINT('Ctrl Pts',(-17.0949617933418,-20.9191620744912,
5.54480186090581));
#152302=CARTESIAN_POINT('Ctrl Pts',(-17.134260768482,-20.9512509900032,
5.54731758544598));
#152303=CARTESIAN_POINT('Ctrl Pts',(-17.1744641402401,-20.9821349467765,
5.54983330998614));
#152304=CARTESIAN_POINT('Ctrl Pts',(-17.1762220465438,-20.9798104602809,
4.74997346007641));
#152305=CARTESIAN_POINT('Ctrl Pts',(-17.6117180223192,-21.3095662889742,
4.77707100605307));
#152306=CARTESIAN_POINT('Ctrl Pts',(-18.9946005733993,-21.8166035361695,
4.8465604875902));
#152307=CARTESIAN_POINT('Ctrl Pts',(-20.9008594909828,-20.8156360190963,
4.94099937082189));
#152308=CARTESIAN_POINT('Ctrl Pts',(-21.288210216193,-19.4541225063383,
5.00834070807693));
#152309=CARTESIAN_POINT('Ctrl Pts',(-21.2903252254699,-18.9508059208324,
5.0332901097715));
#152310=CARTESIAN_POINT('',(-21.2942629789487,-18.9528355653121,4.96670989022851));
#152311=CARTESIAN_POINT('Ctrl Pts',(-17.1735447294247,-20.9833104140831,
4.68319929961578));
#152312=CARTESIAN_POINT('Ctrl Pts',(-17.2909884433531,-21.0753829841412,
4.69063448214821));
#152313=CARTESIAN_POINT('Ctrl Pts',(-18.1310916369067,-21.6211178664512,
4.74046160024112));
#152314=CARTESIAN_POINT('Ctrl Pts',(-20.2331955554845,-21.5817725214897,
4.83268065389451));
#152315=CARTESIAN_POINT('Ctrl Pts',(-21.2762380205877,-19.8928505327429,
4.91974900156632));
#152316=CARTESIAN_POINT('Ctrl Pts',(-21.298094862478,-18.9985742441059,
4.96442541367765));
#152317=CARTESIAN_POINT('Ctrl Pts',(-21.2979001547653,-18.9528367523378,
4.96670989022851));
#152318=CARTESIAN_POINT('Ctrl Pts',(-21.2939998636668,-18.952835479442,
4.96670989022851));
#152319=CARTESIAN_POINT('Ctrl Pts',(-21.2940269378476,-18.8698772454869,
4.97085977152528));
#152320=CARTESIAN_POINT('Ctrl Pts',(-21.2900172964774,-18.7867551328103,
4.97500965282205));
#152321=CARTESIAN_POINT('Ctrl Pts',(-21.2819493183893,-18.7038986680417,
4.97915953411883));
#152322=CARTESIAN_POINT('Ctrl Pts',(-21.273892503302,-18.6211568449806,
4.98330367356456));
#152323=CARTESIAN_POINT('Ctrl Pts',(-21.2617885455565,-18.5386804021309,
4.98744781301029));
#152324=CARTESIAN_POINT('Ctrl Pts',(-21.2456678375727,-18.456899329729,
4.99159195245603));
#152325=CARTESIAN_POINT('Ctrl Pts',(-21.2295645603719,-18.3752066844683,
4.99573161098224));
#152326=CARTESIAN_POINT('Ctrl Pts',(-21.2094532518122,-18.294208373011,
4.99987126950845));
#152327=CARTESIAN_POINT('Ctrl Pts',(-21.1854159920051,-18.2143282341436,
5.00401092803467));
#152328=CARTESIAN_POINT('Ctrl Pts',(-21.1613926712713,-18.1344944173246,
5.00814818599592));
#152329=CARTESIAN_POINT('Ctrl Pts',(-21.1334480518403,-18.0557779336931,
5.01228544395717));
#152330=CARTESIAN_POINT('Ctrl Pts',(-21.1017147974227,-17.9785902003445,
5.01642270191842));
#152331=CARTESIAN_POINT('Ctrl Pts',(-21.069990038471,-17.9014231313041,
5.02055885227397));
#152332=CARTESIAN_POINT('Ctrl Pts',(-21.0344788364885,-17.8257844328049,
5.02469500262952));
#152333=CARTESIAN_POINT('Ctrl Pts',(-20.9953624823967,-17.7520667838548,
5.02883115298507));
#152334=CARTESIAN_POINT('Ctrl Pts',(-20.9562443890682,-17.678345857185,
5.03296748724695));
#152335=CARTESIAN_POINT('Ctrl Pts',(-20.9135210465752,-17.6065465624556,
5.03710382150882));
#152336=CARTESIAN_POINT('Ctrl Pts',(-20.8674196102011,-17.5370368319954,
5.0412401557707));
#152337=CARTESIAN_POINT('Ctrl Pts',(-20.8212714994527,-17.4674567279542,
5.04538067777222));
#152338=CARTESIAN_POINT('Ctrl Pts',(-20.7717387262313,-17.4001712070023,
5.04952119977375));
#152339=CARTESIAN_POINT('Ctrl Pts',(-20.7190913321281,-17.3355185113618,
5.05366172177528));
#152340=CARTESIAN_POINT('Ctrl Pts',(-20.6664157771983,-17.2708312333193,
5.05780445852121));
#152341=CARTESIAN_POINT('Ctrl Pts',(-20.6106225991452,-17.208779931402,
5.06194719526715));
#152342=CARTESIAN_POINT('Ctrl Pts',(-20.5520199344772,-17.1496672011409,
5.06608993201309));
#152343=CARTESIAN_POINT('Ctrl Pts',(-20.493317306161,-17.0904536371683,
5.07023973538444));
#152344=CARTESIAN_POINT('Ctrl Pts',(-20.4317959684771,-17.034188968823,
5.07438953875579));
#152345=CARTESIAN_POINT('Ctrl Pts',(-20.3677981562822,-16.9811363353776,
5.07853934212713));
#152346=CARTESIAN_POINT('Ctrl Pts',(-20.324139169833,-16.9449440949673,
5.08137031717055));
#152347=CARTESIAN_POINT('Ctrl Pts',(-20.2793283343474,-16.9102458437321,
5.08420129221396));
#152348=CARTESIAN_POINT('Ctrl Pts',(-20.2334815623284,-16.8771132454428,
5.08703226725737));
#152349=CARTESIAN_POINT('Ctrl Pts',(-20.1657126925719,-16.8281379601764,
5.09121690165042));
#152350=CARTESIAN_POINT('Ctrl Pts',(-20.0954157767523,-16.7823951726099,
5.09540153604348));
#152351=CARTESIAN_POINT('Ctrl Pts',(-20.0229321512533,-16.7401559934151,
5.09958617043653));
#152352=CARTESIAN_POINT('Ctrl Pts',(-19.9505516972234,-16.6979769364637,
5.10376484852047));
#152353=CARTESIAN_POINT('Ctrl Pts',(-19.8759911100091,-16.6592918118668,
5.10794352660442));
#152354=CARTESIAN_POINT('Ctrl Pts',(-19.799622378274,-16.6243297168797,
5.11212220468837));
#152355=CARTESIAN_POINT('Ctrl Pts',(-19.7218847919079,-16.5887409514667,
5.1163757825738));
#152356=CARTESIAN_POINT('Ctrl Pts',(-19.6422739922292,-16.5570102814913,
5.12062936045924));
#152357=CARTESIAN_POINT('Ctrl Pts',(-19.5612105522305,-16.5293314914585,
5.12488293834467));
#152358=CARTESIAN_POINT('Ctrl Pts',(-19.4817186851985,-16.5021893087812,
5.12905405232263));
#152359=CARTESIAN_POINT('Ctrl Pts',(-19.4008304551545,-16.478943456341,
5.13322516630058));
#152360=CARTESIAN_POINT('Ctrl Pts',(-19.3189628776791,-16.4597282588495,
5.13739628027853));
#152361=CARTESIAN_POINT('Ctrl Pts',(-19.2371227716601,-16.4405195092031,
5.1415659945989));
#152362=CARTESIAN_POINT('Ctrl Pts',(-19.1543044183625,-16.4253388333996,
5.14573570891927));
#152363=CARTESIAN_POINT('Ctrl Pts',(-19.0709381209925,-16.4142701675273,
5.14990542323965));
#152364=CARTESIAN_POINT('Ctrl Pts',(-18.987574790153,-16.4032018955255,
5.1540749891837));
#152365=CARTESIAN_POINT('Ctrl Pts',(-18.9036640101517,-16.3962454022305,
5.15824455512774));
#152366=CARTESIAN_POINT('Ctrl Pts',(-18.8196429975839,-16.3934329641448,
5.16241412107179));
#152367=CARTESIAN_POINT('Ctrl Pts',(-18.7326679098655,-16.3905216442056,
5.16673028381071));
#152368=CARTESIAN_POINT('Ctrl Pts',(-18.6455752209302,-16.3920512290413,
5.17104644654963));
#152369=CARTESIAN_POINT('Ctrl Pts',(-18.5588499153532,-16.3979987376964,
5.17536260928855));
#152370=CARTESIAN_POINT('Ctrl Pts',(-18.4749496774836,-16.4037525068827,
5.17953817348022));
#152371=CARTESIAN_POINT('Ctrl Pts',(-18.3913937177405,-16.413640690019,
5.1837137376719));
#152372=CARTESIAN_POINT('Ctrl Pts',(-18.3086140512034,-16.4275898125371,
5.18788930186358));
#152373=CARTESIAN_POINT('Ctrl Pts',(-18.2216533804996,-16.4422434720727,
5.19227576387612));
#152374=CARTESIAN_POINT('Ctrl Pts',(-18.1355500550634,-16.461378961618,
5.19666222588866));
#152375=CARTESIAN_POINT('Ctrl Pts',(-18.0507884164764,-16.4848514572205,
5.2010486879012));
#152376=CARTESIAN_POINT('Ctrl Pts',(-17.9660267778894,-16.508323952823,
5.20543514991373));
#152377=CARTESIAN_POINT('Ctrl Pts',(-17.8826073525323,-16.5361331988247,
5.20982161192627));
#152378=CARTESIAN_POINT('Ctrl Pts',(-17.8009895271363,-16.5680764572817,
5.21420807393881));
#152379=CARTESIAN_POINT('Ctrl Pts',(-17.7231270588734,-16.5985499590658,
5.21839270833186));
#152380=CARTESIAN_POINT('Ctrl Pts',(-17.6466142262364,-16.6328988372128,
5.2225773427249));
#152381=CARTESIAN_POINT('Ctrl Pts',(-17.5718637493067,-16.6709828289062,
5.22676197711795));
#152382=CARTESIAN_POINT('Ctrl Pts',(-17.4972196704287,-16.7090126127514,
5.23094065520189));
#152383=CARTESIAN_POINT('Ctrl Pts',(-17.4243333709909,-16.7507667429069,
5.23511933328583));
#152384=CARTESIAN_POINT('Ctrl Pts',(-17.3535988359376,-16.7960564417742,
5.23929801136977));
#152385=CARTESIAN_POINT('Ctrl Pts',(-17.2815964351795,-16.8421579259446,
5.24355158925521));
#152386=CARTESIAN_POINT('Ctrl Pts',(-17.2118241472897,-16.8919227999544,
5.24780516714065));
#152387=CARTESIAN_POINT('Ctrl Pts',(-17.144672562554,-16.9451023203508,
5.25205874502608));
#152388=CARTESIAN_POINT('Ctrl Pts',(-17.078822842324,-16.997250851973,5.25622985900404));
#152389=CARTESIAN_POINT('Ctrl Pts',(-17.0154934944014,-17.0526825135667,
5.26040097298199));
#152390=CARTESIAN_POINT('Ctrl Pts',(-16.955023187236,-17.1111193684413,
5.26457208695994));
#152391=CARTESIAN_POINT('Ctrl Pts',(-16.8945731714661,-17.1695366142649,
5.26874180128032));
#152392=CARTESIAN_POINT('Ctrl Pts',(-16.8369806216437,-17.2309567312115,
5.27291151560069));
#152393=CARTESIAN_POINT('Ctrl Pts',(-16.7825490296999,-17.2950633353943,
5.27708122992106));
#152394=CARTESIAN_POINT('Ctrl Pts',(-16.7281193746657,-17.3591676583889,
5.28125079586511));
#152395=CARTESIAN_POINT('Ctrl Pts',(-16.6768507509727,-17.4259579273207,
5.28542036180915));
#152396=CARTESIAN_POINT('Ctrl Pts',(-16.6290069551022,-17.495083982883,
5.28958992775319));
#152397=CARTESIAN_POINT('Ctrl Pts',(-16.5794810303907,-17.5666404252826,
5.29390609049211));
#152398=CARTESIAN_POINT('Ctrl Pts',(-16.5336255484983,-17.6406995292211,
5.29822225323103));
#152399=CARTESIAN_POINT('Ctrl Pts',(-16.4916836990302,-17.7168410602658,
5.30253841596995));
#152400=CARTESIAN_POINT('Ctrl Pts',(-16.4511081008972,-17.7905022889454,
5.30671398016163));
#152401=CARTESIAN_POINT('Ctrl Pts',(-16.414195241831,-17.8661119140595,
5.31088954435331));
#152402=CARTESIAN_POINT('Ctrl Pts',(-16.3811171829163,-17.9432669089039,
5.31506510854499));
#152403=CARTESIAN_POINT('Ctrl Pts',(-16.3463684298814,-18.0243188191194,
5.31945157055753));
#152404=CARTESIAN_POINT('Ctrl Pts',(-16.3158522513522,-18.1070757672222,
5.32383803257007));
#152405=CARTESIAN_POINT('Ctrl Pts',(-16.2897090382153,-18.1910521081324,
5.32822449458261));
#152406=CARTESIAN_POINT('Ctrl Pts',(-16.2635658250785,-18.2750284490425,
5.33261095659515));
#152407=CARTESIAN_POINT('Ctrl Pts',(-16.2417956472861,-18.3602236017744,
5.3369974186077));
#152408=CARTESIAN_POINT('Ctrl Pts',(-16.2244766916358,-18.4461415565825,
5.34138388062024));
#152409=CARTESIAN_POINT('Ctrl Pts',(-16.2079546068079,-18.5281062989289,
5.34556851501329));
#152410=CARTESIAN_POINT('Ctrl Pts',(-16.1954216323759,-18.6110338790213,
5.34975314940633));
#152411=CARTESIAN_POINT('Ctrl Pts',(-16.1869832270606,-18.6945013429833,
5.35393778379938));
#152412=CARTESIAN_POINT('Ctrl Pts',(-16.1785568327709,-18.7778500013415,
5.35811646188332));
#152413=CARTESIAN_POINT('Ctrl Pts',(-16.1742134770096,-18.8617365633852,
5.36229513996725));
#152414=CARTESIAN_POINT('Ctrl Pts',(-16.174007684269,-18.9457275683919,
5.36647381805119));
#152415=CARTESIAN_POINT('Ctrl Pts',(-16.1737982028414,-19.0312240518001,
5.37072739593663));
#152416=CARTESIAN_POINT('Ctrl Pts',(-16.1778761703229,-19.1168282866475,
5.37498097382206));
#152417=CARTESIAN_POINT('Ctrl Pts',(-16.1862438519479,-19.2020772082027,
5.3792345517075));
#152418=CARTESIAN_POINT('Ctrl Pts',(-16.1944493097363,-19.285673413064,
5.38340566568545));
#152419=CARTESIAN_POINT('Ctrl Pts',(-16.2067795899915,-19.3689274796563,
5.3875767796634));
#152420=CARTESIAN_POINT('Ctrl Pts',(-16.2231843067497,-19.4514041995498,
5.39174789364135));
#152421=CARTESIAN_POINT('Ctrl Pts',(-16.2395835187468,-19.5338532435834,
5.39591760796172));
#152422=CARTESIAN_POINT('Ctrl Pts',(-16.2600543622648,-19.615525008144,
5.4000873222821));
#152423=CARTESIAN_POINT('Ctrl Pts',(-16.28449508295,-19.6959930519487,5.40425703660247));
#152424=CARTESIAN_POINT('Ctrl Pts',(-16.3089349339295,-19.7764582323553,
5.40842660254652));
#152425=CARTESIAN_POINT('Ctrl Pts',(-16.3373442466933,-19.8557193372408,
5.41259616849057));
#152426=CARTESIAN_POINT('Ctrl Pts',(-16.3695713807105,-19.9333650209197,
5.41676573443462));
#152427=CARTESIAN_POINT('Ctrl Pts',(-16.4029315810032,-20.0137406310502,
5.42108189717354));
#152428=CARTESIAN_POINT('Ctrl Pts',(-16.4403828646777,-20.0923846228543,
5.42539805991246));
#152429=CARTESIAN_POINT('Ctrl Pts',(-16.4817035150009,-20.1688650474316,
5.42971422265138));
#152430=CARTESIAN_POINT('Ctrl Pts',(-16.5216781494859,-20.2428541302225,
5.43388978684306));
#152431=CARTESIAN_POINT('Ctrl Pts',(-16.5652736482195,-20.3148180591348,
5.43806535103474));
#152432=CARTESIAN_POINT('Ctrl Pts',(-16.6122442629255,-20.3843940073149,
5.44224091522642));
#152433=CARTESIAN_POINT('Ctrl Pts',(-16.6615872517183,-20.4574840712365,
5.44662737723896));
#152434=CARTESIAN_POINT('Ctrl Pts',(-16.714654919849,-20.527938114488,5.45101383925151));
#152435=CARTESIAN_POINT('Ctrl Pts',(-16.7711149075847,-20.5953752200803,
5.45540030126405));
#152436=CARTESIAN_POINT('Ctrl Pts',(-16.8275748953204,-20.6628123256726,
5.45978676327659));
#152437=CARTESIAN_POINT('Ctrl Pts',(-16.8874267520077,-20.7272321203105,
5.46417322528914));
#152438=CARTESIAN_POINT('Ctrl Pts',(-16.9502957329767,-20.788300380603,
5.46855968730168));
#152439=CARTESIAN_POINT('Ctrl Pts',(-17.0102748276393,-20.8465615279686,
5.47274451766204));
#152440=CARTESIAN_POINT('Ctrl Pts',(-17.073223024649,-20.9019893649773,
5.4769293480224));
#152441=CARTESIAN_POINT('Ctrl Pts',(-17.1388417266606,-20.9542662367919,
5.48111417838276));
#152442=CARTESIAN_POINT('Ctrl Pts',(-17.1506303973543,-20.963657992615,
5.48186600043219));
#152443=CARTESIAN_POINT('Ctrl Pts',(-17.1625051568043,-20.9729481370306,
5.48261782248163));
#152444=CARTESIAN_POINT('Ctrl Pts',(-17.1744641402401,-20.9821349467765,
5.48336964453106));
#152445=CARTESIAN_POINT('Origin',(-18.734,-18.952,-1.76670989022851));
#152446=CARTESIAN_POINT('',(-17.1721129507126,-20.9851649608899,6.34984101818205));
#152447=CARTESIAN_POINT('',(-17.1744641402401,-20.9821349467765,6.28334279287586));
#152448=CARTESIAN_POINT('',(-17.1744641402401,-20.9821349467765,-1.76670989022851));
#152449=CARTESIAN_POINT('',(-21.2939994369002,-18.9503020392335,5.8332901097715));
#152450=CARTESIAN_POINT('Ctrl Pts',(-21.2967673690372,-18.950300203358,
5.8332901097715));
#152451=CARTESIAN_POINT('Ctrl Pts',(-21.2975539709192,-18.8475231740461,
5.83841759033362));
#152452=CARTESIAN_POINT('Ctrl Pts',(-21.2452320420947,-17.8958349639979,
5.88593700645621));
#152453=CARTESIAN_POINT('Ctrl Pts',(-20.0538051353946,-16.2277743551153,
5.97584835813928));
#152454=CARTESIAN_POINT('Ctrl Pts',(-17.1577428384119,-16.3676810722738,
6.10302416482072));
#152455=CARTESIAN_POINT('Ctrl Pts',(-15.736433506265,-18.8289532162803,
6.22768838483497));
#152456=CARTESIAN_POINT('Ctrl Pts',(-16.5413044417107,-20.4955798434453,
6.30996066928875));
#152457=CARTESIAN_POINT('Ctrl Pts',(-17.1721129507126,-20.9851649608899,
6.34984101818205));
#152458=CARTESIAN_POINT('Ctrl Pts',(-17.1744641402401,-20.9821349467765,
5.54983330998614));
#152459=CARTESIAN_POINT('Ctrl Pts',(-17.2411773822525,-21.0333836055931,
5.55400788870292));
#152460=CARTESIAN_POINT('Ctrl Pts',(-17.3103822987326,-21.0813118661074,
5.5581824674197));
#152461=CARTESIAN_POINT('Ctrl Pts',(-17.3817082756447,-21.1256851410083,
5.56235704613648));
#152462=CARTESIAN_POINT('Ctrl Pts',(-17.4530769014014,-21.1700849485833,
5.56653412101197));
#152463=CARTESIAN_POINT('Ctrl Pts',(-17.5265687102689,-21.2109253156985,
5.57071119588746));
#152464=CARTESIAN_POINT('Ctrl Pts',(-17.6017887254332,-21.2480177764434,
5.57488827076295));
#152465=CARTESIAN_POINT('Ctrl Pts',(-17.6771346879595,-21.2851723442958,
5.57907233967534));
#152466=CARTESIAN_POINT('Ctrl Pts',(-17.7542142119762,-21.318566294549,
5.58325640858772));
#152467=CARTESIAN_POINT('Ctrl Pts',(-17.8326129636017,-21.3480595590705,
5.58744047750011));
#152468=CARTESIAN_POINT('Ctrl Pts',(-17.8755870423865,-21.364226217938,
5.58973396436506));
#152469=CARTESIAN_POINT('Ctrl Pts',(-17.9189572378514,-21.3792217334331,
5.59202745123002));
#152470=CARTESIAN_POINT('Ctrl Pts',(-17.9626538344086,-21.393029514944,
5.59432093809498));
#152471=CARTESIAN_POINT('Ctrl Pts',(-18.042381468173,-21.4182228213826,
5.59850557248802));
#152472=CARTESIAN_POINT('Ctrl Pts',(-18.123493045634,-21.4395528703719,
5.60269020688107));
#152473=CARTESIAN_POINT('Ctrl Pts',(-18.2055793173495,-21.4568695738795,
5.60687484127412));
#152474=CARTESIAN_POINT('Ctrl Pts',(-18.2875487494174,-21.474161629203,
5.61105351935806));
#152475=CARTESIAN_POINT('Ctrl Pts',(-18.3704896737371,-21.4874515917234,
5.615232197442));
#152476=CARTESIAN_POINT('Ctrl Pts',(-18.4539769469565,-21.4966388918203,
5.61941087552594));
#152477=CARTESIAN_POINT('Ctrl Pts',(-18.5389606695473,-21.5059908676685,
5.62366445341137));
#152478=CARTESIAN_POINT('Ctrl Pts',(-18.624510060566,-21.511091508697,5.62791803129681));
#152479=CARTESIAN_POINT('Ctrl Pts',(-18.7101649534091,-21.5118890387191,
5.63217160918224));
#152480=CARTESIAN_POINT('Ctrl Pts',(-18.7941592590127,-21.5126711070654,
5.63634272316019));
#152481=CARTESIAN_POINT('Ctrl Pts',(-18.87825453103,-21.5093154194064,5.64051383713815));
#152482=CARTESIAN_POINT('Ctrl Pts',(-18.9620126684401,-21.5018255279589,
5.6446849511161));
#152483=CARTESIAN_POINT('Ctrl Pts',(-19.0457426999983,-21.4943381498168,
5.64885466543647));
#152484=CARTESIAN_POINT('Ctrl Pts',(-19.1291353638018,-21.4827193639704,
5.65302437975684));
#152485=CARTESIAN_POINT('Ctrl Pts',(-19.2117557819361,-21.4670247340387,
5.65719409407721));
#152486=CARTESIAN_POINT('Ctrl Pts',(-19.2943732600814,-21.4513306625894,
5.66136366002126));
#152487=CARTESIAN_POINT('Ctrl Pts',(-19.3762180954026,-21.4315611221138,
5.66553322596531));
#152488=CARTESIAN_POINT('Ctrl Pts',(-19.4568650837658,-21.4078228907379,
5.66970279190935));
#152489=CARTESIAN_POINT('Ctrl Pts',(-19.5403475207509,-21.3832500524311,
5.67401895464827));
#152490=CARTESIAN_POINT('Ctrl Pts',(-19.6225458049915,-21.354424401291,
5.6783351173872));
#152491=CARTESIAN_POINT('Ctrl Pts',(-19.7030067527823,-21.3215201862534,
5.68265128012612));
#152492=CARTESIAN_POINT('Ctrl Pts',(-19.7808466936618,-21.2896878225597,
5.6868268443178));
#152493=CARTESIAN_POINT('Ctrl Pts',(-19.8570603406959,-21.2540387751658,
5.69100240850948));
#152494=CARTESIAN_POINT('Ctrl Pts',(-19.9312606656524,-21.2147785791989,
5.69517797270115));
#152495=CARTESIAN_POINT('Ctrl Pts',(-20.009208672628,-21.173535444066,5.6995644347137));
#152496=CARTESIAN_POINT('Ctrl Pts',(-20.0849341253746,-21.1283070744553,
5.70395089672624));
#152497=CARTESIAN_POINT('Ctrl Pts',(-20.1580227463385,-21.0793831854912,
5.70833735873878));
#152498=CARTESIAN_POINT('Ctrl Pts',(-20.2311113673024,-21.0304592965271,
5.71272382075132));
#152499=CARTESIAN_POINT('Ctrl Pts',(-20.3015627371329,-20.977840296355,
5.71711028276386));
#152500=CARTESIAN_POINT('Ctrl Pts',(-20.3690044710744,-20.9218630357379,
5.72149674477641));
#152501=CARTESIAN_POINT('Ctrl Pts',(-20.4324580482223,-20.8691959820087,
5.72562381401755));
#152502=CARTESIAN_POINT('Ctrl Pts',(-20.493497997814,-20.8133485129555,
5.72975088325869));
#152503=CARTESIAN_POINT('Ctrl Pts',(-20.5517814829091,-20.7545732940418,
5.73387795249983));
#152504=CARTESIAN_POINT('Ctrl Pts',(-20.6102782700971,-20.6955829734199,
5.73802012571948));
#152505=CARTESIAN_POINT('Ctrl Pts',(-20.6659979620833,-20.6336436795686,
5.74216229893913));
#152506=CARTESIAN_POINT('Ctrl Pts',(-20.7186255971236,-20.5690532580103,
5.74630447215879));
#152507=CARTESIAN_POINT('Ctrl Pts',(-20.7709257203661,-20.5048647949491,
5.75042086784546));
#152508=CARTESIAN_POINT('Ctrl Pts',(-20.8201718394842,-20.4380584608902,
5.75453726353214));
#152509=CARTESIAN_POINT('Ctrl Pts',(-20.8660914253506,-20.368963709467,
5.75865365921881));
#152510=CARTESIAN_POINT('Ctrl Pts',(-20.9119829684086,-20.299911153783,
5.76276754104798));
#152511=CARTESIAN_POINT('Ctrl Pts',(-20.9545517475122,-20.228573347296,
5.76688142287715));
#152512=CARTESIAN_POINT('Ctrl Pts',(-20.993566969393,-20.1553108953334,
5.77099530470633));
#152513=CARTESIAN_POINT('Ctrl Pts',(-21.0325708263852,-20.0820697842621,
5.77510798818761));
#152514=CARTESIAN_POINT('Ctrl Pts',(-21.0680229592545,-20.006905559054,
5.7792206716689));
#152515=CARTESIAN_POINT('Ctrl Pts',(-21.0997379788823,-19.9302043831808,
5.78333335515018));
#152516=CARTESIAN_POINT('Ctrl Pts',(-21.1318415000294,-19.8525636359715,
5.78749641803529));
#152517=CARTESIAN_POINT('Ctrl Pts',(-21.1601155043872,-19.7733484709675,
5.7916594809204));
#152518=CARTESIAN_POINT('Ctrl Pts',(-21.1844181339265,-19.6929797358392,
5.79582254380551));
#152519=CARTESIAN_POINT('Ctrl Pts',(-21.2084475698834,-19.6135144512045,
5.79993880837766));
#152520=CARTESIAN_POINT('Ctrl Pts',(-21.2285944016387,-19.5329218806182,
5.80405507294981));
#152521=CARTESIAN_POINT('Ctrl Pts',(-21.2447724368935,-19.45162162697,5.80817133752195));
#152522=CARTESIAN_POINT('Ctrl Pts',(-21.2612263672263,-19.3689349046021,
5.81235779956354));
#152523=CARTESIAN_POINT('Ctrl Pts',(-21.2735747867911,-19.2855166404038,
5.81654426160514));
#152524=CARTESIAN_POINT('Ctrl Pts',(-21.281781944964,-19.2018142528271,
5.82073072364673));
#152525=CARTESIAN_POINT('Ctrl Pts',(-21.2899891031369,-19.1181118652504,
5.82491718568832));
#152526=CARTESIAN_POINT('Ctrl Pts',(-21.2940550344004,-19.0341258661346,
5.82910364772991));
#152527=CARTESIAN_POINT('Ctrl Pts',(-21.2939994369002,-18.9503020392335,
5.8332901097715));
#152528=CARTESIAN_POINT('',(-21.2939992944986,-18.9539005700933,5.76670989019962));
#152529=CARTESIAN_POINT('Ctrl Pts',(-17.1744641402401,-20.9821349467765,
5.48336964453106));
#152530=CARTESIAN_POINT('Ctrl Pts',(-17.2409182958941,-21.0331845772146,
5.48754739925117));
#152531=CARTESIAN_POINT('Ctrl Pts',(-17.3099759681969,-21.0810402668187,
5.49172515397129));
#152532=CARTESIAN_POINT('Ctrl Pts',(-17.381296149795,-21.12542869532,5.4959029086914));
#152533=CARTESIAN_POINT('Ctrl Pts',(-17.4525395227181,-21.169769319451,
5.50007616415482));
#152534=CARTESIAN_POINT('Ctrl Pts',(-17.5260401732958,-21.2106498622978,
5.50424941961824));
#152535=CARTESIAN_POINT('Ctrl Pts',(-17.6014265224653,-21.2478391315563,
5.50842267508166));
#152536=CARTESIAN_POINT('Ctrl Pts',(-17.6767685965176,-21.2850065592045,
5.5125934795526));
#152537=CARTESIAN_POINT('Ctrl Pts',(-17.7539937588198,-21.3184868143506,
5.51676428402354));
#152538=CARTESIAN_POINT('Ctrl Pts',(-17.8327051091542,-21.3480942217983,
5.52093508849448));
#152539=CARTESIAN_POINT('Ctrl Pts',(-17.9113938433813,-21.3776931221591,
5.52510469456949));
#152540=CARTESIAN_POINT('Ctrl Pts',(-17.9915674871628,-21.4034212231907,
5.5292743006445));
#152541=CARTESIAN_POINT('Ctrl Pts',(-18.0728096721884,-21.425141190957,
5.53344390671952));
#152542=CARTESIAN_POINT('Ctrl Pts',(-18.154052884509,-21.446861433369,5.53761356551856));
#152543=CARTESIAN_POINT('Ctrl Pts',(-18.2363642201357,-21.4645733243011,
5.5417832243176));
#152544=CARTESIAN_POINT('Ctrl Pts',(-18.3193140098708,-21.4781899234995,
5.54595288311664));
#152545=CARTESIAN_POINT('Ctrl Pts',(-18.4023474046234,-21.4918202468558,
5.55012674451098));
#152546=CARTESIAN_POINT('Ctrl Pts',(-18.4860200839174,-21.5013469583618,
5.55430060590533));
#152547=CARTESIAN_POINT('Ctrl Pts',(-18.5698945442935,-21.5067347023531,
5.55847446729967));
#152548=CARTESIAN_POINT('Ctrl Pts',(-18.6538096081786,-21.5121250545438,
5.56265034925448));
#152549=CARTESIAN_POINT('Ctrl Pts',(-18.7379261871862,-21.5133724408922,
5.56682623120928));
#152550=CARTESIAN_POINT('Ctrl Pts',(-18.8218065112355,-21.5104937007123,
5.57100211316409));
#152551=CARTESIAN_POINT('Ctrl Pts',(-18.9058383997968,-21.5076097588972,
5.57518554057747));
#152552=CARTESIAN_POINT('Ctrl Pts',(-18.9896327207643,-21.5005848307498,
5.57936896799085));
#152553=CARTESIAN_POINT('Ctrl Pts',(-19.0727566144665,-21.4894877253211,
5.58355239540423));
#152554=CARTESIAN_POINT('Ctrl Pts',(-19.1534485520546,-21.4787152879535,
5.58761342826386));
#152555=CARTESIAN_POINT('Ctrl Pts',(-19.2335083856589,-21.4641058242612,
5.59167446112349));
#152556=CARTESIAN_POINT('Ctrl Pts',(-19.3125527301388,-21.4457675790757,
5.59573549398311));
#152557=CARTESIAN_POINT('Ctrl Pts',(-19.394002867067,-21.4268711913428,
5.59992012837616));
#152558=CARTESIAN_POINT('Ctrl Pts',(-19.4746778298126,-21.4039450190917,
5.60410476276921));
#152559=CARTESIAN_POINT('Ctrl Pts',(-19.55414895591,-21.3770681825713,5.60828939716226));
#152560=CARTESIAN_POINT('Ctrl Pts',(-19.6335069646958,-21.3502296019011,
5.61246807524619));
#152561=CARTESIAN_POINT('Ctrl Pts',(-19.7116641083501,-21.3194516726888,
5.61664675333013));
#152562=CARTESIAN_POINT('Ctrl Pts',(-19.7882032486923,-21.2848642288926,
5.62082543141407));
#152563=CARTESIAN_POINT('Ctrl Pts',(-19.8661142981176,-21.2496568300239,
5.62507900929951));
#152564=CARTESIAN_POINT('Ctrl Pts',(-19.9423482986083,-21.2105021111286,
5.62933258718494));
#152565=CARTESIAN_POINT('Ctrl Pts',(-20.0164828014232,-21.1675897327921,
5.63358616507038));
#152566=CARTESIAN_POINT('Ctrl Pts',(-20.0891800622393,-21.1255092946463,
5.63775727904833));
#152567=CARTESIAN_POINT('Ctrl Pts',(-20.1598580881698,-21.0798158370632,
5.64192839302628));
#152568=CARTESIAN_POINT('Ctrl Pts',(-20.2281415862033,-21.0307354137499,
5.64609950700423));
#152569=CARTESIAN_POINT('Ctrl Pts',(-20.2964021710496,-20.9816714598466,
5.6502692213246));
#152570=CARTESIAN_POINT('Ctrl Pts',(-20.3622694505379,-20.929223065652,
5.65443893564497));
#152571=CARTESIAN_POINT('Ctrl Pts',(-20.4253973801082,-20.8736594137784,
5.65860864996535));
#152572=CARTESIAN_POINT('Ctrl Pts',(-20.4885230633159,-20.8180977390979,
5.66277821590939));
#152573=CARTESIAN_POINT('Ctrl Pts',(-20.5489092456568,-20.7594213317294,
5.66694778185343));
#152574=CARTESIAN_POINT('Ctrl Pts',(-20.6062442778982,-20.69793853382,5.67111734779748));
#152575=CARTESIAN_POINT('Ctrl Pts',(-20.6655951391428,-20.6342940765833,
5.6754335105364));
#152576=CARTESIAN_POINT('Ctrl Pts',(-20.721675941672,-20.5676425973541,
5.67974967327532));
#152577=CARTESIAN_POINT('Ctrl Pts',(-20.7741852955293,-20.4983647564226,
5.68406583601424));
#152578=CARTESIAN_POINT('Ctrl Pts',(-20.8249841627078,-20.4313436338727,
5.68824140020592));
#152579=CARTESIAN_POINT('Ctrl Pts',(-20.8724404611871,-20.3618650450199,
5.69241696439761));
#152580=CARTESIAN_POINT('Ctrl Pts',(-20.9163256700509,-20.2903029066086,
5.69659252858929));
#152581=CARTESIAN_POINT('Ctrl Pts',(-20.9624274164872,-20.2151263347089,
5.70097899060183));
#152582=CARTESIAN_POINT('Ctrl Pts',(-21.0045875620258,-20.1376507144178,
5.70536545261437));
#152583=CARTESIAN_POINT('Ctrl Pts',(-21.0425969786766,-20.0583362915702,
5.70975191462691));
#152584=CARTESIAN_POINT('Ctrl Pts',(-21.0806063953274,-19.9790218687226,
5.71413837663946));
#152585=CARTESIAN_POINT('Ctrl Pts',(-21.1144649298774,-19.897869208087,
5.718524838652));
#152586=CARTESIAN_POINT('Ctrl Pts',(-21.144023506431,-19.8153578044185,
5.72291130066454));
#152587=CARTESIAN_POINT('Ctrl Pts',(-21.1768030234138,-19.7238552940413,
5.72777574688623));
#152588=CARTESIAN_POINT('Ctrl Pts',(-21.2043967060823,-19.6304025057852,
5.73264019310792));
#152589=CARTESIAN_POINT('Ctrl Pts',(-21.2266026211961,-19.5355513454757,
5.7375046393296));
#152590=CARTESIAN_POINT('Ctrl Pts',(-21.2488226674987,-19.4406398246877,
5.74237218114127));
#152591=CARTESIAN_POINT('Ctrl Pts',(-21.2656479288596,-19.3443282665163,
5.74723972295294));
#152592=CARTESIAN_POINT('Ctrl Pts',(-21.2769239065511,-19.2471914725919,
5.75210726476461));
#152593=CARTESIAN_POINT('Ctrl Pts',(-21.2881998842426,-19.1500546786674,
5.75697480657628));
#152594=CARTESIAN_POINT('Ctrl Pts',(-21.2939263955806,-19.0520927805187,
5.76184234838795));
#152595=CARTESIAN_POINT('Ctrl Pts',(-21.2939992944986,-18.9539005700933,
5.76670989019962));
#152596=CARTESIAN_POINT('Ctrl Pts',(-21.293999294499,-18.9539005695104,
5.76670989022851));
#152597=CARTESIAN_POINT('Ctrl Pts',(-21.2940618231948,-18.8696766480678,
5.77088500205647));
#152598=CARTESIAN_POINT('Ctrl Pts',(-21.2899635861128,-18.7854119279347,
5.77506011388444));
#152599=CARTESIAN_POINT('Ctrl Pts',(-21.2817191504239,-18.7015461508316,
5.7792352257124));
#152600=CARTESIAN_POINT('Ctrl Pts',(-21.2734754980237,-18.6176883416611,
5.78340994087069));
#152601=CARTESIAN_POINT('Ctrl Pts',(-21.2610864747303,-18.5342298557722,
5.78758465602898));
#152602=CARTESIAN_POINT('Ctrl Pts',(-21.2446185572459,-18.4516056954637,
5.79175937118727));
#152603=CARTESIAN_POINT('Ctrl Pts',(-21.2281473245846,-18.3689649019827,
5.79593492676267));
#152604=CARTESIAN_POINT('Ctrl Pts',(-21.2075956572652,-18.2871592164316,
5.80011048233806));
#152605=CARTESIAN_POINT('Ctrl Pts',(-21.1830809475489,-18.2066125085882,
5.80428603791345));
#152606=CARTESIAN_POINT('Ctrl Pts',(-21.1585369190254,-18.1259694694636,
5.8084665873195));
#152607=CARTESIAN_POINT('Ctrl Pts',(-21.1300205198882,-18.0465888526481,
5.81264713672554));
#152608=CARTESIAN_POINT('Ctrl Pts',(-21.0976986239761,-17.9688780263805,
5.81682768613158));
#152609=CARTESIAN_POINT('Ctrl Pts',(-21.065355928357,-17.8911171918331,
5.8210109257945));
#152610=CARTESIAN_POINT('Ctrl Pts',(-21.0292030575735,-17.8150287001824,
5.82519416545742));
#152611=CARTESIAN_POINT('Ctrl Pts',(-20.9894534545794,-17.740996402059,
5.82937740512034));
#152612=CARTESIAN_POINT('Ctrl Pts',(-20.949632004209,-17.6668302906149,
5.83356820598567));
#152613=CARTESIAN_POINT('Ctrl Pts',(-20.9062010761476,-17.5947281861657,
5.83775900685099));
#152614=CARTESIAN_POINT('Ctrl Pts',(-20.859418003607,-17.5250457926257,
5.84194980771632));
#152615=CARTESIAN_POINT('Ctrl Pts',(-20.8291383592866,-17.4799449051208,
5.84466224092621));
#152616=CARTESIAN_POINT('Ctrl Pts',(-20.7974553185201,-17.435857034571,
5.84737467413609));
#152617=CARTESIAN_POINT('Ctrl Pts',(-20.7644472985012,-17.392870830236,
5.85008710734598));
#152618=CARTESIAN_POINT('Ctrl Pts',(-20.7135238341689,-17.3265534188316,
5.85427174173903));
#152619=CARTESIAN_POINT('Ctrl Pts',(-20.6592531496868,-17.262610070515,
5.85845637613208));
#152620=CARTESIAN_POINT('Ctrl Pts',(-20.6018847443059,-17.2013982228989,
5.86264101052513));
#152621=CARTESIAN_POINT('Ctrl Pts',(-20.5445979957492,-17.1402735027715,
5.86681968860907));
#152622=CARTESIAN_POINT('Ctrl Pts',(-20.4842225962896,-17.0818728934348,
5.87099836669301));
#152623=CARTESIAN_POINT('Ctrl Pts',(-20.4210494366143,-17.0265223453856,
5.87517704477696));
#152624=CARTESIAN_POINT('Ctrl Pts',(-20.3567439434536,-16.9701796785424,
5.87943062266239));
#152625=CARTESIAN_POINT('Ctrl Pts',(-20.2895396974699,-16.9169978755988,
5.88368420054783));
#152626=CARTESIAN_POINT('Ctrl Pts',(-20.2197842460678,-16.867282951061,
5.88793777843326));
#152627=CARTESIAN_POINT('Ctrl Pts',(-20.1513811402077,-16.8185318473461,
5.89210889241121));
#152628=CARTESIAN_POINT('Ctrl Pts',(-20.0805252582504,-16.7731146765032,
5.89628000638917));
#152629=CARTESIAN_POINT('Ctrl Pts',(-20.0075777510545,-16.7312794610715,
5.90045112036712));
#152630=CARTESIAN_POINT('Ctrl Pts',(-19.9346547220991,-16.6894582838504,
5.90462083468749));
#152631=CARTESIAN_POINT('Ctrl Pts',(-19.8596418605523,-16.6512169036013,
5.90879054900787));
#152632=CARTESIAN_POINT('Ctrl Pts',(-19.7829274662086,-16.6167588624227,
5.91296026332824));
#152633=CARTESIAN_POINT('Ctrl Pts',(-19.7062158016923,-16.5823020474091,
5.91712982927229));
#152634=CARTESIAN_POINT('Ctrl Pts',(-19.6278031447566,-16.5516284915072,
5.92129939521634));
#152635=CARTESIAN_POINT('Ctrl Pts',(-19.5480992,-16.5248942147983,5.92546896116038));
#152636=CARTESIAN_POINT('Ctrl Pts',(-19.4655929628713,-16.4972199939008,
5.9297851238993));
#152637=CARTESIAN_POINT('Ctrl Pts',(-19.3817034451241,-16.4737673840696,
5.93410128663822));
#152638=CARTESIAN_POINT('Ctrl Pts',(-19.2969019322694,-16.4546531248848,
5.93841744937714));
#152639=CARTESIAN_POINT('Ctrl Pts',(-19.2148628197764,-16.4361615106825,
5.94259301356882));
#152640=CARTESIAN_POINT('Ctrl Pts',(-19.1319706883696,-16.4217299783601,
5.9467685777605));
#152641=CARTESIAN_POINT('Ctrl Pts',(-19.0486605152116,-16.411411729507,
5.95094414195218));
#152642=CARTESIAN_POINT('Ctrl Pts',(-18.9611425432585,-16.4005723304336,
5.95533060396472));
#152643=CARTESIAN_POINT('Ctrl Pts',(-18.873163771528,-16.3942727005953,
5.95971706597726));
#152644=CARTESIAN_POINT('Ctrl Pts',(-18.7852297301449,-16.3925126461048,
5.9641035279898));
#152645=CARTESIAN_POINT('Ctrl Pts',(-18.6972956887618,-16.3907525916143,
5.96848999000234));
#152646=CARTESIAN_POINT('Ctrl Pts',(-18.609406955249,-16.3935320181048,
5.97287645201488));
#152647=CARTESIAN_POINT('Ctrl Pts',(-18.5220617179687,-16.4007880988421,
5.97726291402742));
#152648=CARTESIAN_POINT('Ctrl Pts',(-18.4387353645322,-16.4077103165486,
5.98144754842047));
#152649=CARTESIAN_POINT('Ctrl Pts',(-18.3555934356669,-16.4187320520138,
5.98563218281352));
#152650=CARTESIAN_POINT('Ctrl Pts',(-18.2730715290517,-16.4338369900522,
5.98981681720658));
#152651=CARTESIAN_POINT('Ctrl Pts',(-18.1906670821564,-16.4489204280809,
5.99399549529053));
#152652=CARTESIAN_POINT('Ctrl Pts',(-18.1088813531835,-16.4680754422336,
5.99817417337448));
#152653=CARTESIAN_POINT('Ctrl Pts',(-18.0281458685296,-16.4912338702985,
6.00235285145843));
#152654=CARTESIAN_POINT('Ctrl Pts',(-17.9459632583371,-16.5148073965427,
6.00660642934386));
#152655=CARTESIAN_POINT('Ctrl Pts',(-17.8648693945427,-16.5425292308518,
6.0108600072293));
#152656=CARTESIAN_POINT('Ctrl Pts',(-17.7853097077367,-16.5742727807073,
6.01511358511473));
#152657=CARTESIAN_POINT('Ctrl Pts',(-17.7072924407073,-16.6054009199064,
6.01928469909268));
#152658=CARTESIAN_POINT('Ctrl Pts',(-17.6307508424361,-16.6403960502736,
6.02345581307064));
#152659=CARTESIAN_POINT('Ctrl Pts',(-17.5560889447382,-16.6790887509865,
6.02762692704859));
#152660=CARTESIAN_POINT('Ctrl Pts',(-17.4814521005611,-16.7177684679901,
6.03179664136896));
#152661=CARTESIAN_POINT('Ctrl Pts',(-17.4086941123775,-16.7601430796846,
6.03596635568934));
#152662=CARTESIAN_POINT('Ctrl Pts',(-17.3381963061949,-16.80599626087,6.04013607000971));
#152663=CARTESIAN_POINT('Ctrl Pts',(-17.2677010086269,-16.8518478104023,
6.04430563595375));
#152664=CARTESIAN_POINT('Ctrl Pts',(-17.1994661183233,-16.9011774317735,
6.04847520189779));
#152665=CARTESIAN_POINT('Ctrl Pts',(-17.1338445888104,-16.9537250789642,
6.05264476784183));
#152666=CARTESIAN_POINT('Ctrl Pts',(-17.0659158872728,-17.0081202366055,
6.05696093058075));
#152667=CARTESIAN_POINT('Ctrl Pts',(-17.0007881489948,-17.0659635923392,
6.06127709331967));
#152668=CARTESIAN_POINT('Ctrl Pts',(-16.9388146313972,-17.1269220585535,
6.06559325605858));
#152669=CARTESIAN_POINT('Ctrl Pts',(-16.8788598946168,-17.1858948091426,
6.06976882025026));
#152670=CARTESIAN_POINT('Ctrl Pts',(-16.8218573212163,-17.2477824589611,
6.07394438444195));
#152671=CARTESIAN_POINT('Ctrl Pts',(-16.7680870902011,-17.3122480580631,
6.07811994863363));
#152672=CARTESIAN_POINT('Ctrl Pts',(-16.7116010526439,-17.3799696613233,
6.08250641064616));
#152673=CARTESIAN_POINT('Ctrl Pts',(-16.6586828203997,-17.4505360152566,
6.0868928726587));
#152674=CARTESIAN_POINT('Ctrl Pts',(-16.6096058643082,-17.5235219440824,
6.09127933467124));
#152675=CARTESIAN_POINT('Ctrl Pts',(-16.5605289082167,-17.5965078729081,
6.09566579668377));
#152676=CARTESIAN_POINT('Ctrl Pts',(-16.5152934615326,-17.671912839942,
6.10005225869631));
#152677=CARTESIAN_POINT('Ctrl Pts',(-16.4741163568267,-17.7492839406919,
6.10443872070885));
#152678=CARTESIAN_POINT('Ctrl Pts',(-16.4348338717473,-17.8230950824048,
6.10862335510189));
#152679=CARTESIAN_POINT('Ctrl Pts',(-16.3990982578627,-17.8989701434485,
6.11280798949494));
#152680=CARTESIAN_POINT('Ctrl Pts',(-16.3671315774458,-17.9765340240092,
6.11699262388799));
#152681=CARTESIAN_POINT('Ctrl Pts',(-16.3352103976416,-18.0539875019866,
6.12117130197194));
#152682=CARTESIAN_POINT('Ctrl Pts',(-16.3070476692933,-18.1331246030379,
6.12534998005589));
#152683=CARTESIAN_POINT('Ctrl Pts',(-16.2828196558216,-18.2135455868414,
6.12952865813984));
#152684=CARTESIAN_POINT('Ctrl Pts',(-16.2581573726208,-18.295408058982,
6.13378223602527));
#152685=CARTESIAN_POINT('Ctrl Pts',(-16.2375724777942,-18.3786004681764,
6.13803581391071));
#152686=CARTESIAN_POINT('Ctrl Pts',(-16.2211996301977,-18.4626797556595,
6.14228939179614));
#152687=CARTESIAN_POINT('Ctrl Pts',(-16.2051442022008,-18.5451290020876,
6.14646050577409));
#152688=CARTESIAN_POINT('Ctrl Pts',(-16.1931390533221,-18.6284305735957,
6.15063161975204));
#152689=CARTESIAN_POINT('Ctrl Pts',(-16.1852604222201,-18.712153039089,
6.15480273372999));
#152690=CARTESIAN_POINT('Ctrl Pts',(-16.1773844348688,-18.7958474107003,
6.15897244805036));
#152691=CARTESIAN_POINT('Ctrl Pts',(-16.1736322583368,-18.8799619381736,
6.16314216237073));
#152692=CARTESIAN_POINT('Ctrl Pts',(-16.1740284019004,-18.9640588939546,
6.1673118766911));
#152693=CARTESIAN_POINT('Ctrl Pts',(-16.1744245313676,-19.0481528572052,
6.17148144263515));
#152694=CARTESIAN_POINT('Ctrl Pts',(-16.1789686844146,-19.1322287899831,
6.1756510085792));
#152695=CARTESIAN_POINT('Ctrl Pts',(-16.1876332505419,-19.2158491562507,
6.17982057452325));
#152696=CARTESIAN_POINT('Ctrl Pts',(-16.1966024521254,-19.3024095114393,
6.18413673726217));
#152697=CARTESIAN_POINT('Ctrl Pts',(-16.2099871509033,-19.3884811440158,
6.18845290000109));
#152698=CARTESIAN_POINT('Ctrl Pts',(-16.2276984844482,-19.4735867263867,
6.19276906274001));
#152699=CARTESIAN_POINT('Ctrl Pts',(-16.2448328731658,-19.5559200033635,
6.19694462693169));
#152700=CARTESIAN_POINT('Ctrl Pts',(-16.2660161808878,-19.6373487577952,
6.20112019112337));
#152701=CARTESIAN_POINT('Ctrl Pts',(-16.2911167416149,-19.7174550188626,
6.20529575531506));
#152702=CARTESIAN_POINT('Ctrl Pts',(-16.3174850719935,-19.8016072567419,
6.2096822173276));
#152703=CARTESIAN_POINT('Ctrl Pts',(-16.3481765728436,-19.8842993445549,
6.21406867934013));
#152704=CARTESIAN_POINT('Ctrl Pts',(-16.3829817631982,-19.965071197017,
6.21845514135267));
#152705=CARTESIAN_POINT('Ctrl Pts',(-16.4177869535528,-20.045843049479,
6.22284160336521));
#152706=CARTESIAN_POINT('Ctrl Pts',(-16.4567055084016,-20.1246941799628,
6.22722806537775));
#152707=CARTESIAN_POINT('Ctrl Pts',(-16.4994739740983,-20.2011971179794,
6.23161452739029));
#152708=CARTESIAN_POINT('Ctrl Pts',(-16.5415036429151,-20.27637851848,6.23592521618075));
#152709=CARTESIAN_POINT('Ctrl Pts',(-16.5874123872811,-20.3495805439044,
6.24023590497122));
#152710=CARTESIAN_POINT('Ctrl Pts',(-16.6369860440941,-20.4203774953111,
6.24454659376168));
#152711=CARTESIAN_POINT('Ctrl Pts',(-16.6850336766682,-20.4889951065029,
6.24872458676161));
#152712=CARTESIAN_POINT('Ctrl Pts',(-16.7365236132887,-20.5553531244434,
6.25290257976153));
#152713=CARTESIAN_POINT('Ctrl Pts',(-16.7912139159174,-20.619087949538,
6.25708057276145));
#152714=CARTESIAN_POINT('Ctrl Pts',(-16.8485097182233,-20.6858591642344,
6.26145760944719));
#152715=CARTESIAN_POINT('Ctrl Pts',(-16.9093181745504,-20.7497505671933,
6.26583464613292));
#152716=CARTESIAN_POINT('Ctrl Pts',(-16.973310673513,-20.8103791581899,
6.27021168281866));
#152717=CARTESIAN_POINT('Ctrl Pts',(-17.0373031724756,-20.8710077491866,
6.27458871950439));
#152718=CARTESIAN_POINT('Ctrl Pts',(-17.1044793276203,-20.9283730896681,
6.27896575619013));
#152719=CARTESIAN_POINT('Ctrl Pts',(-17.1744641402401,-20.9821349467765,
6.28334279287586));
#152720=CARTESIAN_POINT('Origin',(-18.734,-18.952,-1.76670989022851));
#152721=CARTESIAN_POINT('',(-17.1744641402401,-20.9821349467765,7.14996297217343));
#152722=CARTESIAN_POINT('',(-17.1744641402401,-20.9821349467765,7.08324141939143));
#152723=CARTESIAN_POINT('',(-17.1744641402401,-20.9821349467765,-1.76670989022851));
#152724=CARTESIAN_POINT('',(-21.2939991231355,-18.954118854712,6.6332901097715));
#152725=CARTESIAN_POINT('Ctrl Pts',(-21.2939991231355,-18.954118854712,
6.6332901097715));
#152726=CARTESIAN_POINT('Ctrl Pts',(-21.2940674480299,-18.8715687540988,
6.63740642252224));
#152727=CARTESIAN_POINT('Ctrl Pts',(-21.2901386830331,-18.788875859184,
6.64152273527298));
#152728=CARTESIAN_POINT('Ctrl Pts',(-21.2821979940262,-18.7064659224447,
6.64563904802373));
#152729=CARTESIAN_POINT('Ctrl Pts',(-21.2742662779566,-18.6241491085059,
6.64975070936244));
#152730=CARTESIAN_POINT('Ctrl Pts',(-21.2623316869624,-18.5421150878493,
6.65386237070115));
#152731=CARTESIAN_POINT('Ctrl Pts',(-21.2464314307689,-18.4607889397778,
6.65797403203986));
#152732=CARTESIAN_POINT('Ctrl Pts',(-21.2305407999848,-18.3795120234587,
6.66208320433541));
#152733=CARTESIAN_POINT('Ctrl Pts',(-21.2106893569247,-18.2989425946371,
6.66619237663095));
#152734=CARTESIAN_POINT('Ctrl Pts',(-21.1869659077107,-18.2194986309849,
6.6703015489265));
#152735=CARTESIAN_POINT('Ctrl Pts',(-21.1632492097462,-18.1400772755973,
6.67440955182855));
#152736=CARTESIAN_POINT('Ctrl Pts',(-21.1356628286737,-18.0617812045221,
6.67851755473059));
#152737=CARTESIAN_POINT('Ctrl Pts',(-21.1043458531986,-17.9850147176796,
6.68262555763264));
#152738=CARTESIAN_POINT('Ctrl Pts',(-21.0730277445932,-17.9082454532244,
6.686733709173));
#152739=CARTESIAN_POINT('Ctrl Pts',(-21.0379789552763,-17.8330063217982,
6.69084186071337));
#152740=CARTESIAN_POINT('Ctrl Pts',(-20.9993866849094,-17.7596815996408,
6.69495001225373));
#152741=CARTESIAN_POINT('Ctrl Pts',(-20.9607561733792,-17.6862842198592,
6.69906223457025));
#152742=CARTESIAN_POINT('Ctrl Pts',(-20.9185753946451,-17.6148054564872,
6.70317445688677));
#152743=CARTESIAN_POINT('Ctrl Pts',(-20.8730771242598,-17.5456042319217,
6.70728667920329));
#152744=CARTESIAN_POINT('Ctrl Pts',(-20.8275541489319,-17.4763654320317,
6.71140113440064));
#152745=CARTESIAN_POINT('Ctrl Pts',(-20.7787103793543,-17.4094070139061,
6.715515589598));
#152746=CARTESIAN_POINT('Ctrl Pts',(-20.7268199445207,-17.3450561090317,
6.71963004479535));
#152747=CARTESIAN_POINT('Ctrl Pts',(-20.6748438133914,-17.2805989295771,
6.72375129495541));
#152748=CARTESIAN_POINT('Ctrl Pts',(-20.6198112918954,-17.2187582108668,
6.72787254511546));
#152749=CARTESIAN_POINT('Ctrl Pts',(-20.5620341095491,-17.1598249822283,
6.73199379527552));
#152750=CARTESIAN_POINT('Ctrl Pts',(-20.529745700387,-17.1268905239828,
6.73429692959298));
#152751=CARTESIAN_POINT('Ctrl Pts',(-20.4966007367167,-17.0948633881749,
6.73660006391043));
#152752=CARTESIAN_POINT('Ctrl Pts',(-20.4626578964191,-17.0637887096122,
6.73890319822789));
#152753=CARTESIAN_POINT('Ctrl Pts',(-20.400986123379,-17.0073281863674,
6.74308783262094));
#152754=CARTESIAN_POINT('Ctrl Pts',(-20.3364305466714,-16.9537872066972,
6.74727246701399));
#152755=CARTESIAN_POINT('Ctrl Pts',(-20.2692989765721,-16.9034744198481,
6.75145710140703));
#152756=CARTESIAN_POINT('Ctrl Pts',(-20.2022629599536,-16.8532332470236,
6.75563577949098));
#152757=CARTESIAN_POINT('Ctrl Pts',(-20.1326585979523,-16.8062114135715,
6.75981445757492));
#152758=CARTESIAN_POINT('Ctrl Pts',(-20.0608289916761,-16.7626793686516,
6.76399313565886));
#152759=CARTESIAN_POINT('Ctrl Pts',(-19.9877118913304,-16.7183670431124,
6.7682467135443));
#152760=CARTESIAN_POINT('Ctrl Pts',(-19.9122893426568,-16.6776711711576,
6.77250029142973));
#152761=CARTESIAN_POINT('Ctrl Pts',(-19.8349567777298,-16.6408327248832,
6.77675386931517));
#152762=CARTESIAN_POINT('Ctrl Pts',(-19.7591234554761,-16.6047084637741,
6.78092498329312));
#152763=CARTESIAN_POINT('Ctrl Pts',(-19.6814539493098,-16.5722936025649,
6.78509609727107));
#152764=CARTESIAN_POINT('Ctrl Pts',(-19.6023470115176,-16.5437696398416,
6.78926721124902));
#152765=CARTESIAN_POINT('Ctrl Pts',(-19.5232666188221,-16.5152552486095,
6.7934369255694));
#152766=CARTESIAN_POINT('Ctrl Pts',(-19.4427501848433,-16.4906293187766,
6.79760663988977));
#152767=CARTESIAN_POINT('Ctrl Pts',(-19.3612154692012,-16.4700248278448,
6.80177635421015));
#152768=CARTESIAN_POINT('Ctrl Pts',(-19.2796836549143,-16.4494210701093,
6.8059459201542));
#152769=CARTESIAN_POINT('Ctrl Pts',(-19.1971340772289,-16.4328385786397,
6.81011548609824));
#152770=CARTESIAN_POINT('Ctrl Pts',(-19.1139973178551,-16.4203598126071,
6.81428505204228));
#152771=CARTESIAN_POINT('Ctrl Pts',(-19.0279375725819,-16.407442308555,
6.8186012147812));
#152772=CARTESIAN_POINT('Ctrl Pts',(-18.9412491083339,-16.3989225513938,
6.82291737752012));
#152773=CARTESIAN_POINT('Ctrl Pts',(-18.8544163259003,-16.3948336173693,
6.82723354025904));
#152774=CARTESIAN_POINT('Ctrl Pts',(-18.7704121122212,-16.3908778799405,
6.83140910445072));
#152775=CARTESIAN_POINT('Ctrl Pts',(-18.6862733092299,-16.3910686822566,
6.8355846686424));
#152776=CARTESIAN_POINT('Ctrl Pts',(-18.6024375216844,-16.3953828377523,
6.83976023283408));
#152777=CARTESIAN_POINT('Ctrl Pts',(-18.5143673878107,-16.3999148909862,
6.84414669484662));
#152778=CARTESIAN_POINT('Ctrl Pts',(-18.4266322652435,-16.4089977253143,
6.84853315685916));
#152779=CARTESIAN_POINT('Ctrl Pts',(-18.3397299608672,-16.4225433120446,
6.8529196188717));
#152780=CARTESIAN_POINT('Ctrl Pts',(-18.252827656491,-16.4360888987749,
6.85730608088424));
#152781=CARTESIAN_POINT('Ctrl Pts',(-18.1667587226473,-16.4540970446291,
6.86169254289678));
#152782=CARTESIAN_POINT('Ctrl Pts',(-18.0820028534405,-16.4764193164273,
6.86607900490932));
#152783=CARTESIAN_POINT('Ctrl Pts',(-18.0011467274143,-16.4977145074105,
6.87026363930236));
#152784=CARTESIAN_POINT('Ctrl Pts',(-17.921184527277,-16.5230148144695,
6.87444827369541));
#152785=CARTESIAN_POINT('Ctrl Pts',(-17.8425423900642,-16.5522284838578,
6.87863290808845));
#152786=CARTESIAN_POINT('Ctrl Pts',(-17.7640121901998,-16.5814005712036,
6.88281158617239));
#152787=CARTESIAN_POINT('Ctrl Pts',(-17.6867987486329,-16.6144747979096,
6.88699026425634));
#152788=CARTESIAN_POINT('Ctrl Pts',(-17.6113151844297,-16.6513090592416,
6.89116894234028));
#152789=CARTESIAN_POINT('Ctrl Pts',(-17.5344786315872,-16.6888035482357,
6.89542252022572));
#152790=CARTESIAN_POINT('Ctrl Pts',(-17.4594350484393,-16.7301940721622,
6.89967609811116));
#152791=CARTESIAN_POINT('Ctrl Pts',(-17.3866010942662,-16.7752785688501,
6.90392967599659));
#152792=CARTESIAN_POINT('Ctrl Pts',(-17.3151791684184,-16.8194890145946,
6.90810078997454));
#152793=CARTESIAN_POINT('Ctrl Pts',(-17.2458823693353,-16.8672512282385,
6.9122719039525));
#152794=CARTESIAN_POINT('Ctrl Pts',(-17.1790791456547,-16.9183281639551,
6.91644301793045));
#152795=CARTESIAN_POINT('Ctrl Pts',(-17.112298338441,-16.9693879603127,
6.92061273225082));
#152796=CARTESIAN_POINT('Ctrl Pts',(-17.0480098099917,-17.0237599905361,
6.9247824465712));
#152797=CARTESIAN_POINT('Ctrl Pts',(-16.9865514987007,-17.0811649630962,
6.92895216089157));
#152798=CARTESIAN_POINT('Ctrl Pts',(-16.92509537436,-17.1385678929411,6.93312172683562));
#152799=CARTESIAN_POINT('Ctrl Pts',(-16.8664696025457,-17.1990032359,6.93729129277967));
#152800=CARTESIAN_POINT('Ctrl Pts',(-16.8109765840841,-17.2621535744811,
6.94146085872371));
#152801=CARTESIAN_POINT('Ctrl Pts',(-16.7535324995514,-17.3275242010623,
6.94577702146263));
#152802=CARTESIAN_POINT('Ctrl Pts',(-16.699445910539,-17.3958038977866,
6.95009318420155));
#152803=CARTESIAN_POINT('Ctrl Pts',(-16.6490068258948,-17.4666032637929,
6.95440934694047));
#152804=CARTESIAN_POINT('Ctrl Pts',(-16.6002107891277,-17.5350963478982,
6.95858491113215));
#152805=CARTESIAN_POINT('Ctrl Pts',(-16.5548284854398,-17.6059470436345,
6.96276047532383));
#152806=CARTESIAN_POINT('Ctrl Pts',(-16.5130772857549,-17.6787748442046,
6.96693603951551));
#152807=CARTESIAN_POINT('Ctrl Pts',(-16.469217332228,-17.7552810038499,
6.97132250152805));
#152808=CARTESIAN_POINT('Ctrl Pts',(-16.4293652006908,-17.833968723497,
6.97570896354059));
#152809=CARTESIAN_POINT('Ctrl Pts',(-16.3937163263691,-17.9143717780744,
6.98009542555314));
#152810=CARTESIAN_POINT('Ctrl Pts',(-16.3580674520473,-17.9947748326518,
6.98448188756568));
#152811=CARTESIAN_POINT('Ctrl Pts',(-16.3266219713967,-18.0768926531097,
6.98886834957822));
#152812=CARTESIAN_POINT('Ctrl Pts',(-16.2995147249234,-18.1602415485545,
6.99325481159076));
#152813=CARTESIAN_POINT('Ctrl Pts',(-16.273654723043,-18.2397554377671,
6.99743944598381));
#152814=CARTESIAN_POINT('Ctrl Pts',(-16.251646255088,-18.3206855701428,
7.00162408037685));
#152815=CARTESIAN_POINT('Ctrl Pts',(-16.233642830573,-18.4026239673095,
7.00580871476989));
#152816=CARTESIAN_POINT('Ctrl Pts',(-16.2156650317043,-18.4844457353099,
7.00998739285384));
#152817=CARTESIAN_POINT('Ctrl Pts',(-16.2016810508027,-18.5672724719893,
7.01416607093779));
#152818=CARTESIAN_POINT('Ctrl Pts',(-16.1917950137905,-18.6506798909933,
7.01834474902174));
#152819=CARTESIAN_POINT('Ctrl Pts',(-16.1817317766699,-18.7355823280391,
7.02259832690717));
#152820=CARTESIAN_POINT('Ctrl Pts',(-16.1759149888559,-18.8210860111299,
7.02685190479261));
#152821=CARTESIAN_POINT('Ctrl Pts',(-16.1744002778054,-18.9067312233285,
7.03110548267805));
#152822=CARTESIAN_POINT('Ctrl Pts',(-16.1729149323844,-18.9907160359657,
7.035276596656));
#152823=CARTESIAN_POINT('Ctrl Pts',(-16.1755663524988,-19.0748364579018,
7.03944771063395));
#152824=CARTESIAN_POINT('Ctrl Pts',(-16.1823546543812,-19.1586543737305,
7.0436188246119));
#152825=CARTESIAN_POINT('Ctrl Pts',(-16.1891406783834,-19.2424441636481,
7.04778853893228));
#152826=CARTESIAN_POINT('Ctrl Pts',(-16.2000607901197,-19.3259311909065,
7.05195825325265));
#152827=CARTESIAN_POINT('Ctrl Pts',(-16.2150630692561,-19.408680127589,
7.05612796757302));
#152828=CARTESIAN_POINT('Ctrl Pts',(-16.2300648145471,-19.4914261197094,
7.06029753351707));
#152829=CARTESIAN_POINT('Ctrl Pts',(-16.2491483555178,-19.5734336209725,
7.06446709946112));
#152830=CARTESIAN_POINT('Ctrl Pts',(-16.2722104781218,-19.6542765480713,
7.06863666540517));
#152831=CARTESIAN_POINT('Ctrl Pts',(-16.2960834365064,-19.7379618127562,
7.07295282814409));
#152832=CARTESIAN_POINT('Ctrl Pts',(-16.3242198111562,-19.8203985795373,
7.07726899088301));
#152833=CARTESIAN_POINT('Ctrl Pts',(-16.3564491538598,-19.9011322215678,
7.08158515362193));
#152834=CARTESIAN_POINT('Ctrl Pts',(-16.3876286291149,-19.9792359737009,
7.08576071781361));
#152835=CARTESIAN_POINT('Ctrl Pts',(-16.4226382716206,-20.0557454470094,
7.08993628200529));
#152836=CARTESIAN_POINT('Ctrl Pts',(-16.4612757941355,-20.1302719058339,
7.09411184619697));
#152837=CARTESIAN_POINT('Ctrl Pts',(-16.5018648060606,-20.2085625189238,
7.0984983082095));
#152838=CARTESIAN_POINT('Ctrl Pts',(-16.5464575227366,-20.2846640250243,
7.10288477022204));
#152839=CARTESIAN_POINT('Ctrl Pts',(-16.5947677080408,-20.3581597352503,
7.10727123223458));
#152840=CARTESIAN_POINT('Ctrl Pts',(-16.6430778933451,-20.4316554454763,
7.11165769424711));
#152841=CARTESIAN_POINT('Ctrl Pts',(-16.6951051426579,-20.5025449370744,
7.11604415625965));
#152842=CARTESIAN_POINT('Ctrl Pts',(-16.7505157350918,-20.5704530178111,
7.12043061827219));
#152843=CARTESIAN_POINT('Ctrl Pts',(-16.8033793819778,-20.6352397064761,
7.12461545674303));
#152844=CARTESIAN_POINT('Ctrl Pts',(-16.8595189473533,-20.6975542088439,
7.12880029521386));
#152845=CARTESIAN_POINT('Ctrl Pts',(-16.9186744386697,-20.7570465662638,
7.1329851336847));
#152846=CARTESIAN_POINT('Ctrl Pts',(-16.9777385242717,-20.8164469974515,
7.13716350583869));
#152847=CARTESIAN_POINT('Ctrl Pts',(-17.0398089529806,-20.8730336264076,
7.14134187799268));
#152848=CARTESIAN_POINT('Ctrl Pts',(-17.1045853939782,-20.9264893116152,
7.14552025014667));
#152849=CARTESIAN_POINT('Ctrl Pts',(-17.127543594814,-20.9454351866573,
7.14700115748892));
#152850=CARTESIAN_POINT('Ctrl Pts',(-17.1508413505485,-20.9639880803871,
7.14848206483117));
#152851=CARTESIAN_POINT('Ctrl Pts',(-17.1744641402401,-20.9821349467765,
7.14996297217343));
#152852=CARTESIAN_POINT('Ctrl Pts',(-17.1721129507126,-20.9851649608899,
6.34984101818205));
#152853=CARTESIAN_POINT('Ctrl Pts',(-17.2118400414908,-21.015998077639,
6.35235260484923));
#152854=CARTESIAN_POINT('Ctrl Pts',(-17.9391679507452,-21.5446793877424,
6.39725612707689));
#152855=CARTESIAN_POINT('Ctrl Pts',(-19.9200692482785,-21.7370548823945,
6.48455158486502));
#152856=CARTESIAN_POINT('Ctrl Pts',(-21.2201491927466,-20.0919179991473,
6.57652302872766));
#152857=CARTESIAN_POINT('Ctrl Pts',(-21.2969228070761,-19.0983559330699,
6.62610253702982));
#152858=CARTESIAN_POINT('Ctrl Pts',(-21.2956373923518,-18.9541202106712,
6.6332901097715));
#152859=CARTESIAN_POINT('',(-21.293999428374,-18.9502892327451,6.5667098902584));
#152860=CARTESIAN_POINT('Ctrl Pts',(-17.1744641402401,-20.9821349467765,
6.28334279287586));
#152861=CARTESIAN_POINT('Ctrl Pts',(-17.2411328275767,-21.0333493789942,
6.28751243024914));
#152862=CARTESIAN_POINT('Ctrl Pts',(-17.3103496505638,-21.0812937513021,
6.29168206762242));
#152863=CARTESIAN_POINT('Ctrl Pts',(-17.3817564935579,-21.1257151375664,
6.2958517049957));
#152864=CARTESIAN_POINT('Ctrl Pts',(-17.4531631314398,-21.1701363962327,
6.30002133039193));
#152865=CARTESIAN_POINT('Ctrl Pts',(-17.5267593855407,-21.2110344470256,
6.30419095578816));
#152866=CARTESIAN_POINT('Ctrl Pts',(-17.6021596903972,-21.2482006692705,
6.30836058118439));
#152867=CARTESIAN_POINT('Ctrl Pts',(-17.6781541019692,-21.285659737841,
6.31256306059166));
#152868=CARTESIAN_POINT('Ctrl Pts',(-17.7559807011725,-21.319327685251,
6.31676553999894));
#152869=CARTESIAN_POINT('Ctrl Pts',(-17.8352228079875,-21.3490397491736,
6.32096801940622));
#152870=CARTESIAN_POINT('Ctrl Pts',(-17.9139612308849,-21.3785629553113,
6.32514378673608));
#152871=CARTESIAN_POINT('Ctrl Pts',(-17.9940967580289,-21.4041803383333,
6.32931955406594));
#152872=CARTESIAN_POINT('Ctrl Pts',(-18.0752056469976,-21.4257805077355,
6.33349532139579));
#152873=CARTESIAN_POINT('Ctrl Pts',(-18.1570928073895,-21.4475879391874,
6.33771115684178));
#152874=CARTESIAN_POINT('Ctrl Pts',(-18.2399716399031,-21.4653005516914,
6.34192699228777));
#152875=CARTESIAN_POINT('Ctrl Pts',(-18.3233977108253,-21.4788568934794,
6.34614282773376));
#152876=CARTESIAN_POINT('Ctrl Pts',(-18.4068237817474,-21.4924132352675,
6.35035866317974));
#152877=CARTESIAN_POINT('Ctrl Pts',(-18.4907966114,-21.5018133172571,6.35457449862573));
#152878=CARTESIAN_POINT('Ctrl Pts',(-18.5748705298082,-21.5070494734381,
6.35879033407172));
#152879=CARTESIAN_POINT('Ctrl Pts',(-18.6583222240302,-21.512246877256,
6.36297496846476));
#152880=CARTESIAN_POINT('Ctrl Pts',(-18.742184118471,-21.5133611702432,
6.36715960285781));
#152881=CARTESIAN_POINT('Ctrl Pts',(-18.8260228331339,-21.5103455197025,
6.37134423725085));
#152882=CARTESIAN_POINT('Ctrl Pts',(-18.9097422137639,-21.5073341615672,
6.3755229153348));
#152883=CARTESIAN_POINT('Ctrl Pts',(-18.993438024348,-21.5002045527773,
6.37970159341875));
#152884=CARTESIAN_POINT('Ctrl Pts',(-19.0766734176215,-21.4889617515555,
6.3838802715027));
#152885=CARTESIAN_POINT('Ctrl Pts',(-19.1614007454992,-21.4775174312018,
6.38813384938813));
#152886=CARTESIAN_POINT('Ctrl Pts',(-19.2456505065471,-21.4618109801083,
6.39238742727357));
#152887=CARTESIAN_POINT('Ctrl Pts',(-19.3289636478329,-21.4419032627308,
6.396641005159));
#152888=CARTESIAN_POINT('Ctrl Pts',(-19.4106616013027,-21.4223814953013,
6.40081211913695));
#152889=CARTESIAN_POINT('Ctrl Pts',(-19.4914584592903,-21.3988200192302,
6.4049832331149));
#152890=CARTESIAN_POINT('Ctrl Pts',(-19.5709299408016,-21.3713280625392,
6.40915434709285));
#152891=CARTESIAN_POINT('Ctrl Pts',(-19.6503747548898,-21.3438453310398,
6.41332406141322));
#152892=CARTESIAN_POINT('Ctrl Pts',(-19.7284946413759,-21.3124348885695,
6.41749377573359));
#152893=CARTESIAN_POINT('Ctrl Pts',(-19.8048810053293,-21.2772556574332,
6.42166349005396));
#152894=CARTESIAN_POINT('Ctrl Pts',(-19.8812646511281,-21.2420776781249,
6.425833055998));
#152895=CARTESIAN_POINT('Ctrl Pts',(-19.9559144795494,-21.2031313700067,
6.43000262194205));
#152896=CARTESIAN_POINT('Ctrl Pts',(-20.0284436491277,-21.1606230188135,
6.43417218788609));
#152897=CARTESIAN_POINT('Ctrl Pts',(-20.103522854834,-21.1166201264321,
6.43848835062501));
#152898=CARTESIAN_POINT('Ctrl Pts',(-20.176329047329,-21.068800314323,6.44280451336393));
#152899=CARTESIAN_POINT('Ctrl Pts',(-20.2464645244673,-21.0174420984932,
6.44712067610285));
#152900=CARTESIAN_POINT('Ctrl Pts',(-20.3143153458147,-20.9677568711422,
6.45129624029453));
#152901=CARTESIAN_POINT('Ctrl Pts',(-20.3796664407516,-20.9147605602811,
6.45547180448621));
#152902=CARTESIAN_POINT('Ctrl Pts',(-20.4421918593798,-20.8587460689742,
6.45964736867789));
#152903=CARTESIAN_POINT('Ctrl Pts',(-20.507875288263,-20.7999024188731,
6.46403383069043));
#152904=CARTESIAN_POINT('Ctrl Pts',(-20.5704396751017,-20.7377280904825,
6.46842029270298));
#152905=CARTESIAN_POINT('Ctrl Pts',(-20.6295529524491,-20.6726042556212,
6.47280675471552));
#152906=CARTESIAN_POINT('Ctrl Pts',(-20.6886662297964,-20.6074804207598,
6.47719321672807));
#152907=CARTESIAN_POINT('Ctrl Pts',(-20.7443280892574,-20.5394075767508,
6.48157967874061));
#152908=CARTESIAN_POINT('Ctrl Pts',(-20.7962584977303,-20.4688025212726,
6.48596614075316));
#152909=CARTESIAN_POINT('Ctrl Pts',(-20.8460908704135,-20.4010499743282,
6.49017538570612));
#152910=CARTESIAN_POINT('Ctrl Pts',(-20.8926734978047,-20.3307132360494,
6.49438463065908));
#152911=CARTESIAN_POINT('Ctrl Pts',(-20.9357293738869,-20.2581346654015,
6.49859387561203));
#152912=CARTESIAN_POINT('Ctrl Pts',(-20.978722858141,-20.1856612676154,
6.50279702099133));
#152913=CARTESIAN_POINT('Ctrl Pts',(-21.0181995127225,-20.1109528753409,
6.50700016637063));
#152914=CARTESIAN_POINT('Ctrl Pts',(-21.0539239335175,-20.0343829926107,
6.51120331174993));
#152915=CARTESIAN_POINT('Ctrl Pts',(-21.0896068791139,-19.9579020056841,
6.51540157737791));
#152916=CARTESIAN_POINT('Ctrl Pts',(-21.1215460556627,-19.8795642299174,
6.51959984300589));
#152917=CARTESIAN_POINT('Ctrl Pts',(-21.1495512259748,-19.7997689984256,
6.52379810863387));
#152918=CARTESIAN_POINT('Ctrl Pts',(-21.1775306085271,-19.7200472440895,
6.52799250840908));
#152919=CARTESIAN_POINT('Ctrl Pts',(-21.2015830381501,-19.6388711282236,
6.53218690818428));
#152920=CARTESIAN_POINT('Ctrl Pts',(-21.2215663308332,-19.556660028202,
6.53638130795949));
#152921=CARTESIAN_POINT('Ctrl Pts',(-21.2415389226779,-19.4744929513404,
6.54057346167872));
#152922=CARTESIAN_POINT('Ctrl Pts',(-21.2574466025637,-19.391292431292,
6.54476561539796));
#152923=CARTESIAN_POINT('Ctrl Pts',(-21.2691973211301,-19.3074919730945,
6.54895776911719));
#152924=CARTESIAN_POINT('Ctrl Pts',(-21.2809466969546,-19.2237010906845,
6.55314944380356));
#152925=CARTESIAN_POINT('Ctrl Pts',(-21.288539988214,-19.1393108539585,
6.55734111848993));
#152926=CARTESIAN_POINT('Ctrl Pts',(-21.2919366299884,-19.0547628189733,
6.5615327931763));
#152927=CARTESIAN_POINT('Ctrl Pts',(-21.2933350165072,-19.0199546642823,
6.5632584921937));
#152928=CARTESIAN_POINT('Ctrl Pts',(-21.294022704555,-18.985119821685,6.56498419121111));
#152929=CARTESIAN_POINT('Ctrl Pts',(-21.2939994283744,-18.9502892333484,
6.56670989022851));
#152930=CARTESIAN_POINT('Ctrl Pts',(-21.293999428374,-18.9502892327451,
6.5667098902584));
#152931=CARTESIAN_POINT('Ctrl Pts',(-21.2939356382109,-18.8548333601135,
6.57143929947811));
#152932=CARTESIAN_POINT('Ctrl Pts',(-21.2885288437516,-18.7595846663126,
6.57616870869782));
#152933=CARTESIAN_POINT('Ctrl Pts',(-21.2778724975473,-18.6650980721178,
6.58089811791753));
#152934=CARTESIAN_POINT('Ctrl Pts',(-21.2671635859909,-18.5701453968674,
6.5856508562461));
#152935=CARTESIAN_POINT('Ctrl Pts',(-21.2511533349016,-18.4759625571734,
6.59040359457466));
#152936=CARTESIAN_POINT('Ctrl Pts',(-21.2299860493113,-18.383094347327,
6.59515633290323));
#152937=CARTESIAN_POINT('Ctrl Pts',(-21.2086961910769,-18.2896883688573,
6.59993659274375));
#152938=CARTESIAN_POINT('Ctrl Pts',(-21.1821895164639,-18.1976124823347,
6.60471685258427));
#152939=CARTESIAN_POINT('Ctrl Pts',(-21.1506609174307,-18.1073994967067,
6.60949711242479));
#152940=CARTESIAN_POINT('Ctrl Pts',(-21.1426476472041,-18.0844710744505,
6.61071205742805));
#152941=CARTESIAN_POINT('Ctrl Pts',(-21.1343102131572,-18.061662873534,
6.61192700243132));
#152942=CARTESIAN_POINT('Ctrl Pts',(-21.1256522921827,-18.0389833992214,
6.61314194743458));
#152943=CARTESIAN_POINT('Ctrl Pts',(-21.0958318198278,-17.9608684985716,
6.61732658182763));
#152944=CARTESIAN_POINT('Ctrl Pts',(-21.062124806143,-17.8840707367778,
6.62151121622068));
#152945=CARTESIAN_POINT('Ctrl Pts',(-21.0246680532229,-17.8090039939071,
6.62569585061373));
#152946=CARTESIAN_POINT('Ctrl Pts',(-20.9872646153543,-17.7340440992535,
6.62987452869768));
#152947=CARTESIAN_POINT('Ctrl Pts',(-20.9461222434272,-17.6608107375728,
6.63405320678162));
#152948=CARTESIAN_POINT('Ctrl Pts',(-20.9014264094921,-17.5896994606784,
6.63823188486557));
#152949=CARTESIAN_POINT('Ctrl Pts',(-20.8559294348561,-17.5173135652524,
6.64248546275101));
#152950=CARTESIAN_POINT('Ctrl Pts',(-20.8067505255347,-17.4471270300727,
6.64673904063645));
#152951=CARTESIAN_POINT('Ctrl Pts',(-20.7541351457543,-17.3795325145211,
6.65099261852188));
#152952=CARTESIAN_POINT('Ctrl Pts',(-20.7025398177813,-17.3132484505532,
6.65516373249984));
#152953=CARTESIAN_POINT('Ctrl Pts',(-20.6476403712485,-17.2494571801025,
6.65933484647779));
#152954=CARTESIAN_POINT('Ctrl Pts',(-20.5897118973504,-17.188499686977,
6.66350596045574));
#152955=CARTESIAN_POINT('Ctrl Pts',(-20.5318028619112,-17.127562648727,
6.66767567477611));
#152956=CARTESIAN_POINT('Ctrl Pts',(-20.4708671343697,-17.0694578324914,
6.67184538909649));
#152957=CARTESIAN_POINT('Ctrl Pts',(-20.4072185463107,-17.0144913687206,
6.67601510341686));
#152958=CARTESIAN_POINT('Ctrl Pts',(-20.3435722231415,-16.9595268608925,
6.6801846693609));
#152959=CARTESIAN_POINT('Ctrl Pts',(-20.2772135801197,-16.9077007835214,
6.68435423530495));
#152960=CARTESIAN_POINT('Ctrl Pts',(-20.2084905554454,-16.8592798558091,
6.68852380124899));
#152961=CARTESIAN_POINT('Ctrl Pts',(-20.1373513140027,-16.8091565080122,
6.69283996398791));
#152962=CARTESIAN_POINT('Ctrl Pts',(-20.0636787652557,-16.7626825189766,
6.69715612672683));
#152963=CARTESIAN_POINT('Ctrl Pts',(-19.9878910926204,-16.7201045885062,
6.70147228946575));
#152964=CARTESIAN_POINT('Ctrl Pts',(-19.9145721954497,-16.6789136296424,
6.70564785365743));
#152965=CARTESIAN_POINT('Ctrl Pts',(-19.8392743011541,-16.6413689670526,
6.70982341784911));
#152966=CARTESIAN_POINT('Ctrl Pts',(-19.7623989816003,-16.607646030429,
6.71399898204079));
#152967=CARTESIAN_POINT('Ctrl Pts',(-19.6816408724096,-16.5722198284451,
6.71838544405333));
#152968=CARTESIAN_POINT('Ctrl Pts',(-19.5991423447411,-16.5410117758973,
6.72277190606587));
#152969=CARTESIAN_POINT('Ctrl Pts',(-19.5153878511231,-16.5141663251737,
6.72715836807841));
#152970=CARTESIAN_POINT('Ctrl Pts',(-19.4316333575051,-16.48732087445,6.73154483009095));
#152971=CARTESIAN_POINT('Ctrl Pts',(-19.3466234783172,-16.4648381003647,
6.73593129210349));
#152972=CARTESIAN_POINT('Ctrl Pts',(-19.2608535512399,-16.4468003401833,
6.74031775411602));
#152973=CARTESIAN_POINT('Ctrl Pts',(-19.1790300256488,-16.4295925240862,
6.74450238850907));
#152974=CARTESIAN_POINT('Ctrl Pts',(-19.0962102942859,-16.4163656164703,
6.74868702290212));
#152975=CARTESIAN_POINT('Ctrl Pts',(-19.0128164131692,-16.407228613854,
6.75287165729517));
#152976=CARTESIAN_POINT('Ctrl Pts',(-18.92954123292,-16.3981046166299,6.75705033537912));
#152977=CARTESIAN_POINT('Ctrl Pts',(-18.8456939795802,-16.3930590108019,
6.76122901346306));
#152978=CARTESIAN_POINT('Ctrl Pts',(-18.76170764213,-16.3921499484213,6.76540769154701));
#152979=CARTESIAN_POINT('Ctrl Pts',(-18.6762159099409,-16.3912245917508,
6.76966126943245));
#152980=CARTESIAN_POINT('Ctrl Pts',(-18.5905805302509,-16.3945856314592,
6.77391484731788));
#152981=CARTESIAN_POINT('Ctrl Pts',(-18.5052645325904,-16.4022392100534,
6.77816842520332));
#152982=CARTESIAN_POINT('Ctrl Pts',(-18.421602552025,-16.4097444090919,
6.78233953918127));
#152983=CARTESIAN_POINT('Ctrl Pts',(-18.3382481596055,-16.4213771508025,
6.78651065315922));
#152984=CARTESIAN_POINT('Ctrl Pts',(-18.2556369703987,-16.4370906950924,
6.79068176713718));
#152985=CARTESIAN_POINT('Ctrl Pts',(-18.1730535021743,-16.4527989665509,
6.79485148145755));
#152986=CARTESIAN_POINT('Ctrl Pts',(-18.0912131934259,-16.472585235142,
6.79902119577792));
#152987=CARTESIAN_POINT('Ctrl Pts',(-18.0105433225007,-16.4963513207745,
6.8031909100983));
#152988=CARTESIAN_POINT('Ctrl Pts',(-17.9298763221558,-16.5201165607077,
6.80736047604234));
#152989=CARTESIAN_POINT('Ctrl Pts',(-17.8503801178648,-16.5478612052845,
6.81153004198638));
#152990=CARTESIAN_POINT('Ctrl Pts',(-17.7724673106158,-16.579437063586,
6.81569960793043));
#152991=CARTESIAN_POINT('Ctrl Pts',(-17.6918151851798,-16.6121230901123,
6.82001577066935));
#152992=CARTESIAN_POINT('Ctrl Pts',(-17.6128603617428,-16.6489145558588,
6.82433193340827));
#152993=CARTESIAN_POINT('Ctrl Pts',(-17.5360366305501,-16.6895933686766,
6.82864809614719));
#152994=CARTESIAN_POINT('Ctrl Pts',(-17.4617154243205,-16.7289470734455,
6.83282366033887));
#152995=CARTESIAN_POINT('Ctrl Pts',(-17.3893889826095,-16.771938472629,
6.83699922453055));
#152996=CARTESIAN_POINT('Ctrl Pts',(-17.3194221772607,-16.8183248646023,
6.84117478872223));
#152997=CARTESIAN_POINT('Ctrl Pts',(-17.2459215149041,-16.867054122961,
6.84556125073476));
#152998=CARTESIAN_POINT('Ctrl Pts',(-17.1750255931742,-16.9195300021187,
6.8499477127473));
#152999=CARTESIAN_POINT('Ctrl Pts',(-17.1071180986344,-16.9754233435029,
6.85433417475984));
#153000=CARTESIAN_POINT('Ctrl Pts',(-17.0392106040947,-17.0313166848872,
6.85872063677238));
#153001=CARTESIAN_POINT('Ctrl Pts',(-16.9742919138006,-17.0906270409863,
6.86310709878492));
#153002=CARTESIAN_POINT('Ctrl Pts',(-16.9126993772538,-17.1529824788001,
6.86749356079746));
#153003=CARTESIAN_POINT('Ctrl Pts',(-16.8539408046155,-17.2124688504872,
6.8716781951905));
#153004=CARTESIAN_POINT('Ctrl Pts',(-16.7979903187279,-17.2749476638324,
6.87586282958355));
#153005=CARTESIAN_POINT('Ctrl Pts',(-16.7451680193311,-17.3401230342645,
6.8800474639766));
#153006=CARTESIAN_POINT('Ctrl Pts',(-16.6924209059394,-17.4052056356239,
6.88422614206054));
#153007=CARTESIAN_POINT('Ctrl Pts',(-16.6427934219785,-17.47297681583,6.88840482014449));
#153008=CARTESIAN_POINT('Ctrl Pts',(-16.5965688328438,-17.5431039762746,
6.89258349822843));
#153009=CARTESIAN_POINT('Ctrl Pts',(-16.5495157011698,-17.6144881156707,
6.89683707611387));
#153010=CARTESIAN_POINT('Ctrl Pts',(-16.5059889968457,-17.6883131849443,
6.9010906539993));
#153011=CARTESIAN_POINT('Ctrl Pts',(-16.4662445138507,-17.7641931743589,
6.90534423188474));
#153012=CARTESIAN_POINT('Ctrl Pts',(-16.4272705552134,-17.8386020821111,
6.90951534586269));
#153013=CARTESIAN_POINT('Ctrl Pts',(-16.3919336983951,-17.9149865174728,
6.91368645984064));
#153014=CARTESIAN_POINT('Ctrl Pts',(-16.3604304325482,-17.9929548975848,
6.9178575738186));
#153015=CARTESIAN_POINT('Ctrl Pts',(-16.3289377379263,-18.0708971146538,
6.92202728813897));
#153016=CARTESIAN_POINT('Ctrl Pts',(-16.3012762516654,-18.1504217947137,
6.92619700245934));
#153017=CARTESIAN_POINT('Ctrl Pts',(-16.277594697511,-18.2311165212713,
6.93036671677971));
#153018=CARTESIAN_POINT('Ctrl Pts',(-16.253913986048,-18.3118083763642,
6.93453628272376));
#153019=CARTESIAN_POINT('Ctrl Pts',(-16.2342130538339,-18.3936697535164,
6.9387058486678));
#153020=CARTESIAN_POINT('Ctrl Pts',(-16.2185906288469,-18.4762735076588,
6.94287541461184));
#153021=CARTESIAN_POINT('Ctrl Pts',(-16.2024189386697,-18.5617815078941,
6.94719157735076));
#153022=CARTESIAN_POINT('Ctrl Pts',(-16.190617990557,-18.6480845421363,
6.95150774008969));
#153023=CARTESIAN_POINT('Ctrl Pts',(-16.1832392059578,-18.7346998122939,
6.95582390282861));
#153024=CARTESIAN_POINT('Ctrl Pts',(-16.1761007844907,-18.8184935991364,
6.95999946702029));
#153025=CARTESIAN_POINT('Ctrl Pts',(-16.1731008165489,-18.9025791196894,
6.96417503121196));
#153026=CARTESIAN_POINT('Ctrl Pts',(-16.1742327266829,-18.9865182046884,
6.96835059540364));
#153027=CARTESIAN_POINT('Ctrl Pts',(-16.1754218069069,-19.0746968533245,
6.97273705741619));
#153028=CARTESIAN_POINT('Ctrl Pts',(-16.1811710990057,-19.1627133020808,
6.97712351942873));
#153029=CARTESIAN_POINT('Ctrl Pts',(-16.1914115149699,-19.2500667639851,
6.98150998144128));
#153030=CARTESIAN_POINT('Ctrl Pts',(-16.2016519309342,-19.3374202258893,
6.98589644345382));
#153031=CARTESIAN_POINT('Ctrl Pts',(-16.2163832985703,-19.4241101416678,
6.99028290546636));
#153032=CARTESIAN_POINT('Ctrl Pts',(-16.2354754819719,-19.5096515334977,
6.9946693674789));
#153033=CARTESIAN_POINT('Ctrl Pts',(-16.2536851821504,-19.5912390117506,
6.99885307745135));
#153034=CARTESIAN_POINT('Ctrl Pts',(-16.2759292313602,-19.6720854131194,
7.00303678742379));
#153035=CARTESIAN_POINT('Ctrl Pts',(-16.3021321571724,-19.7517617113997,
7.00722049739624));
#153036=CARTESIAN_POINT('Ctrl Pts',(-16.3283004575831,-19.8313327228186,
7.01139867887776));
#153037=CARTESIAN_POINT('Ctrl Pts',(-16.3584171062948,-19.9097362680112,
7.01557686035929));
#153038=CARTESIAN_POINT('Ctrl Pts',(-16.3923558259102,-19.9865542817808,
7.01975504184081));
#153039=CARTESIAN_POINT('Ctrl Pts',(-16.4262598829414,-20.0632938391182,
7.0239289560262));
#153040=CARTESIAN_POINT('Ctrl Pts',(-16.4639780734803,-20.1384506626445,
7.0281028702116));
#153041=CARTESIAN_POINT('Ctrl Pts',(-16.5053350197151,-20.2116239143695,
7.032276784397));
#153042=CARTESIAN_POINT('Ctrl Pts',(-16.5474166561144,-20.2860793675301,
7.0365238373132));
#153043=CARTESIAN_POINT('Ctrl Pts',(-16.5932656311566,-20.3584806089359,
7.0407708902294));
#153044=CARTESIAN_POINT('Ctrl Pts',(-16.6426471430979,-20.4284292153461,
7.0450179431456));
#153045=CARTESIAN_POINT('Ctrl Pts',(-16.6911293175254,-20.4971039157272,
7.04918764861211));
#153046=CARTESIAN_POINT('Ctrl Pts',(-16.7430161416243,-20.5634141925112,
7.05335735407862));
#153047=CARTESIAN_POINT('Ctrl Pts',(-16.7980413928969,-20.6270117228197,
7.05752705954513));
#153048=CARTESIAN_POINT('Ctrl Pts',(-16.8545977101723,-20.692378840986,
7.06181278618618));
#153049=CARTESIAN_POINT('Ctrl Pts',(-16.9144694015651,-20.7548795964524,
7.06609851282723));
#153050=CARTESIAN_POINT('Ctrl Pts',(-16.9773239709915,-20.8141732811709,
7.07038423946828));
#153051=CARTESIAN_POINT('Ctrl Pts',(-17.0401785404178,-20.8734669658894,
7.07466996610933));
#153052=CARTESIAN_POINT('Ctrl Pts',(-17.1060155888496,-20.9295532350968,
7.07895569275038));
#153053=CARTESIAN_POINT('Ctrl Pts',(-17.1744641402401,-20.9821349467765,
7.08324141939143));
#153054=CARTESIAN_POINT('Origin',(-18.734,-18.952,-1.76670989022851));
#153055=CARTESIAN_POINT('',(-17.1770150605606,-20.9788230109682,7.94987221524758));
#153056=CARTESIAN_POINT('',(-17.1718944119046,-20.9854718354472,7.88329695584275));
#153057=CARTESIAN_POINT('',(-17.1744641402401,-20.9821349467765,-1.76670989022851));
#153058=CARTESIAN_POINT('',(-21.29363549648,-18.9525601738873,7.43329008494618));
#153059=CARTESIAN_POINT('Ctrl Pts',(-21.2898970146452,-18.9525588546298,
7.4332901097715));
#153060=CARTESIAN_POINT('Ctrl Pts',(-21.288997505724,-18.4906083046144,
7.4561794192865));
#153061=CARTESIAN_POINT('Ctrl Pts',(-20.9482575273653,-17.1718695394144,
7.52146066436198));
#153062=CARTESIAN_POINT('Ctrl Pts',(-18.8327965306519,-15.9265198389028,
7.62913384499793));
#153063=CARTESIAN_POINT('Ctrl Pts',(-16.2435266653506,-17.2312927241795,
7.75630965167936));
#153064=CARTESIAN_POINT('Ctrl Pts',(-15.9876142035043,-19.6552910609173,
7.86322244176258));
#153065=CARTESIAN_POINT('Ctrl Pts',(-16.8231471588985,-20.7063099151551,
7.92774329628532));
#153066=CARTESIAN_POINT('Ctrl Pts',(-17.1770150605606,-20.9788230109682,
7.94987221524758));
#153067=CARTESIAN_POINT('Ctrl Pts',(-17.1744641402401,-20.9821349467765,
7.14996297217343));
#153068=CARTESIAN_POINT('Ctrl Pts',(-17.2410258191382,-21.0332671758395,
7.15413570876718));
#153069=CARTESIAN_POINT('Ctrl Pts',(-17.3101704637236,-21.0811728588169,
7.15830844536094));
#153070=CARTESIAN_POINT('Ctrl Pts',(-17.3815499321768,-21.1255866244631,
7.16248118195469));
#153071=CARTESIAN_POINT('Ctrl Pts',(-17.4528912216783,-21.1699766343845,
7.16665168666424));
#153072=CARTESIAN_POINT('Ctrl Pts',(-17.5264645719111,-21.2108781927614,
7.17082219137378));
#153073=CARTESIAN_POINT('Ctrl Pts',(-17.601892368295,-21.2480688818577,
7.17499269608332));
#153074=CARTESIAN_POINT('Ctrl Pts',(-17.6773024471275,-21.2852508350771,
7.17916222116552));
#153075=CARTESIAN_POINT('Ctrl Pts',(-17.7545656943623,-21.3187234472259,
7.18333174624772));
#153076=CARTESIAN_POINT('Ctrl Pts',(-17.8332805880677,-21.3483106102858,
7.18750127132992));
#153077=CARTESIAN_POINT('Ctrl Pts',(-17.9120006044927,-21.3778996988611,
7.1916710677624));
#153078=CARTESIAN_POINT('Ctrl Pts',(-17.992172023889,-21.4036026756203,
7.19584086419487));
#153079=CARTESIAN_POINT('Ctrl Pts',(-18.0733753666637,-21.4252923591499,
7.20001066062734));
#153080=CARTESIAN_POINT('Ctrl Pts',(-18.1546631662148,-21.447004601366,
7.20418479392025));
#153081=CARTESIAN_POINT('Ctrl Pts',(-18.2369845870321,-21.46469509586,7.20835892721316));
#153082=CARTESIAN_POINT('Ctrl Pts',(-18.3199075506605,-21.4782872844156,
7.21253306050607));
#153083=CARTESIAN_POINT('Ctrl Pts',(-18.4028745562677,-21.4918866920436,
7.21670941076135));
#153084=CARTESIAN_POINT('Ctrl Pts',(-18.4864432835453,-21.5013834070713,
7.22088576101664));
#153085=CARTESIAN_POINT('Ctrl Pts',(-18.5701765131517,-21.5067527992267,
7.22506211127192));
#153086=CARTESIAN_POINT('Ctrl Pts',(-18.6540563452631,-21.5121315922657,
7.22924577359927));
#153087=CARTESIAN_POINT('Ctrl Pts',(-18.7381007944719,-21.5133686209315,
7.23342943592662));
#153088=CARTESIAN_POINT('Ctrl Pts',(-18.8218728097775,-21.5104914245121,
7.23761309825396));
#153089=CARTESIAN_POINT('Ctrl Pts',(-18.8885736292776,-21.5082005477994,
7.24094420715385));
#153090=CARTESIAN_POINT('Ctrl Pts',(-18.9551017008547,-21.5033024409368,
7.24427531605374));
#153091=CARTESIAN_POINT('Ctrl Pts',(-19.0212404493959,-21.4958342957494,
7.24760642495362));
#153092=CARTESIAN_POINT('Ctrl Pts',(-19.1043258393297,-21.4864525978996,
7.25179105934667));
#153093=CARTESIAN_POINT('Ctrl Pts',(-19.1871057341708,-21.4729786230522,
7.25597569373973));
#153094=CARTESIAN_POINT('Ctrl Pts',(-19.2691452086517,-21.455441552275,
7.26016032813278));
#153095=CARTESIAN_POINT('Ctrl Pts',(-19.3510679100953,-21.4379294433474,
7.26433900621674));
#153096=CARTESIAN_POINT('Ctrl Pts',(-19.4322518385276,-21.416365821315,
7.26851768430069));
#153097=CARTESIAN_POINT('Ctrl Pts',(-19.512267670395,-21.3908315713099,
7.27269636238465));
#153098=CARTESIAN_POINT('Ctrl Pts',(-19.5937177285419,-21.3648396382247,
7.27694994027009));
#153099=CARTESIAN_POINT('Ctrl Pts',(-19.6739569228745,-21.3347333841331,
7.28120351815552));
#153100=CARTESIAN_POINT('Ctrl Pts',(-19.7525437584813,-21.3006525098573,
7.28545709604095));
#153101=CARTESIAN_POINT('Ctrl Pts',(-19.8296070349302,-21.2672323598327,
7.2896282100189));
#153102=CARTESIAN_POINT('Ctrl Pts',(-19.9050810078239,-21.2299905173575,
7.29379932399685));
#153103=CARTESIAN_POINT('Ctrl Pts',(-19.9785668286285,-21.1891082694133,
7.29797043797479));
#153104=CARTESIAN_POINT('Ctrl Pts',(-20.0520279905563,-21.1482397399023,
7.30214015229516));
#153105=CARTESIAN_POINT('Ctrl Pts',(-20.1235019236783,-21.1037334544492,
7.30630986661553));
#153106=CARTESIAN_POINT('Ctrl Pts',(-20.1926138614935,-21.055816912913,
7.3104795809359));
#153107=CARTESIAN_POINT('Ctrl Pts',(-20.2617233400095,-21.007902076453,
7.31464914687995));
#153108=CARTESIAN_POINT('Ctrl Pts',(-20.3284706127606,-20.9565774880018,
7.31881871282399));
#153109=CARTESIAN_POINT('Ctrl Pts',(-20.392510565395,-20.9021135106637,
7.32298827876804));
#153110=CARTESIAN_POINT('Ctrl Pts',(-20.4588020837621,-20.8457346470711,
7.32730444150696));
#153111=CARTESIAN_POINT('Ctrl Pts',(-20.5221919593127,-20.7859918669765,
7.33162060424587));
#153112=CARTESIAN_POINT('Ctrl Pts',(-20.5823369324964,-20.7232285521552,
7.33593676698479));
#153113=CARTESIAN_POINT('Ctrl Pts',(-20.6405226895048,-20.6625097457126,
7.34011233117647));
#153114=CARTESIAN_POINT('Ctrl Pts',(-20.6956714299406,-20.598964557046,
7.34428789536816));
#153115=CARTESIAN_POINT('Ctrl Pts',(-20.7475130548919,-20.5329380689262,
7.34846345955984));
#153116=CARTESIAN_POINT('Ctrl Pts',(-20.8019730770776,-20.4635767398546,
7.35284992157237));
#153117=CARTESIAN_POINT('Ctrl Pts',(-20.8527827827186,-20.3914773402457,
7.35723638358491));
#153118=CARTESIAN_POINT('Ctrl Pts',(-20.8996813854344,-20.3170729419277,
7.36162284559745));
#153119=CARTESIAN_POINT('Ctrl Pts',(-20.9465799881501,-20.2426685436096,
7.36600930760998));
#153120=CARTESIAN_POINT('Ctrl Pts',(-20.9895672706481,-20.1659596899256,
7.37039576962252));
#153121=CARTESIAN_POINT('Ctrl Pts',(-21.0284398795321,-20.0874054955005,
7.37478223163505));
#153122=CARTESIAN_POINT('Ctrl Pts',(-21.0682036058612,-20.0070505211677,
7.37926924910127));
#153123=CARTESIAN_POINT('Ctrl Pts',(-21.103794382086,-19.9244993534847,
7.38375626656748));
#153124=CARTESIAN_POINT('Ctrl Pts',(-21.1349820909847,-19.8401919830593,
7.38824328403369));
#153125=CARTESIAN_POINT('Ctrl Pts',(-21.1660643193882,-19.7561697500644,
7.39271512587973));
#153126=CARTESIAN_POINT('Ctrl Pts',(-21.1927730322953,-19.6704034844231,
7.39718696772577));
#153127=CARTESIAN_POINT('Ctrl Pts',(-21.2149257129941,-19.5833537887784,
7.40165880957181));
#153128=CARTESIAN_POINT('Ctrl Pts',(-21.2370311427379,-19.4964897673327,
7.40612111312314));
#153129=CARTESIAN_POINT('Ctrl Pts',(-21.2545997969947,-19.4083481090824,
7.41058341667445));
#153130=CARTESIAN_POINT('Ctrl Pts',(-21.2674980351242,-19.3194067310512,
7.41504572022578));
#153131=CARTESIAN_POINT('Ctrl Pts',(-21.2803582069864,-19.2307278436205,
7.41949485428542));
#153132=CARTESIAN_POINT('Ctrl Pts',(-21.2885753721633,-19.1412542906272,
7.42394398834506));
#153133=CARTESIAN_POINT('Ctrl Pts',(-21.292066600817,-19.0514749505384,
7.4283931224047));
#153134=CARTESIAN_POINT('Ctrl Pts',(-21.2933474798422,-19.0185362676211,
7.43002544244517));
#153135=CARTESIAN_POINT('Ctrl Pts',(-21.2939927168564,-18.9855565464178,
7.43165776248564));
#153136=CARTESIAN_POINT('Ctrl Pts',(-21.2939999386838,-18.9525603024938,
7.43329008252611));
#153137=CARTESIAN_POINT('',(-21.2941233546374,-18.9508698167174,7.36670989022851));
#153138=CARTESIAN_POINT('Ctrl Pts',(-17.1744641402401,-20.9821349467765,
7.08324141939143));
#153139=CARTESIAN_POINT('Ctrl Pts',(-17.2411540116663,-21.0333656524678,
7.08741703089603));
#153140=CARTESIAN_POINT('Ctrl Pts',(-17.3103223783338,-21.0812695113244,
7.09159264240062));
#153141=CARTESIAN_POINT('Ctrl Pts',(-17.3815967344457,-21.1256157450935,
7.09576825390522));
#153142=CARTESIAN_POINT('Ctrl Pts',(-17.4557821042021,-21.171773184163,
7.10011440728107));
#153143=CARTESIAN_POINT('Ctrl Pts',(-17.5322486915606,-21.2140758921702,
7.10446056065693));
#153144=CARTESIAN_POINT('Ctrl Pts',(-17.6105502174091,-21.2523174967809,
7.10880671403278));
#153145=CARTESIAN_POINT('Ctrl Pts',(-17.6888517432577,-21.2905591013917,
7.11315286740862));
#153146=CARTESIAN_POINT('Ctrl Pts',(-17.7689876693612,-21.3247394525465,
7.11749902078447));
#153147=CARTESIAN_POINT('Ctrl Pts',(-17.8504927560597,-21.3547099179687,
7.12184517416032));
#153148=CARTESIAN_POINT('Ctrl Pts',(-17.9289688151197,-21.3835665710906,
7.12602980855337));
#153149=CARTESIAN_POINT('Ctrl Pts',(-18.009006152961,-21.4086281659991,
7.13021444294641));
#153150=CARTESIAN_POINT('Ctrl Pts',(-18.0902029058993,-21.429725832619,
7.13439907733946));
#153151=CARTESIAN_POINT('Ctrl Pts',(-18.1712840853099,-21.4507934693218,
7.1385777554234));
#153152=CARTESIAN_POINT('Ctrl Pts',(-18.2535209603944,-21.4679082701427,
7.14275643350735));
#153153=CARTESIAN_POINT('Ctrl Pts',(-18.3364934985373,-21.4809500946628,
7.14693511159129));
#153154=CARTESIAN_POINT('Ctrl Pts',(-18.4209532597952,-21.4942256845144,
7.15118868947672));
#153155=CARTESIAN_POINT('Ctrl Pts',(-18.5061748645251,-21.5032806792605,
7.15544226736216));
#153156=CARTESIAN_POINT('Ctrl Pts',(-18.5917010358988,-21.508042058499,
7.1596958452476));
#153157=CARTESIAN_POINT('Ctrl Pts',(-18.6755691155499,-21.5127111291099,
7.16386695922555));
#153158=CARTESIAN_POINT('Ctrl Pts',(-18.7597295775161,-21.5132515520536,
7.1680380732035));
#153159=CARTESIAN_POINT('Ctrl Pts',(-18.8437446259187,-21.5096465973785,
7.17220918718145));
#153160=CARTESIAN_POINT('Ctrl Pts',(-18.9277314822606,-21.5060428523808,
7.17637890150182));
#153161=CARTESIAN_POINT('Ctrl Pts',(-19.0115725627189,-21.4982965120596,
7.1805486158222));
#153162=CARTESIAN_POINT('Ctrl Pts',(-19.0948308836174,-21.4864429513066,
7.18471833014257));
#153163=CARTESIAN_POINT('Ctrl Pts',(-19.1780862418277,-21.4745898123542,
7.18888789608662));
#153164=CARTESIAN_POINT('Ctrl Pts',(-19.2607584263887,-21.4586298092437,
7.19305746203066));
#153165=CARTESIAN_POINT('Ctrl Pts',(-19.3424177464727,-21.4386499242509,
7.19722702797471));
#153166=CARTESIAN_POINT('Ctrl Pts',(-19.4269481075131,-21.4179675711496,
7.20154319071363));
#153167=CARTESIAN_POINT('Ctrl Pts',(-19.5103925419325,-21.3929775239273,
7.20585935345255));
#153168=CARTESIAN_POINT('Ctrl Pts',(-19.5922902863026,-21.363832868264,
7.21017551619147));
#153169=CARTESIAN_POINT('Ctrl Pts',(-19.6715202202639,-21.3356375966935,
7.21435108038315));
#153170=CARTESIAN_POINT('Ctrl Pts',(-19.7493022661266,-21.3035544560161,
7.21852664457483));
#153171=CARTESIAN_POINT('Ctrl Pts',(-19.8252402968867,-21.2677708467054,
7.22270220876651));
#153172=CARTESIAN_POINT('Ctrl Pts',(-19.9050137770549,-21.2301798923559,
7.22708867077905));
#153173=CARTESIAN_POINT('Ctrl Pts',(-19.9827515495241,-21.1885050997007,
7.23147513279159));
#153174=CARTESIAN_POINT('Ctrl Pts',(-20.058026370739,-21.1430166976971,
7.23586159480413));
#153175=CARTESIAN_POINT('Ctrl Pts',(-20.133301191954,-21.0975282956936,
7.24024805681667));
#153176=CARTESIAN_POINT('Ctrl Pts',(-20.2061126241217,-21.0482266726393,
7.24463451882921));
#153177=CARTESIAN_POINT('Ctrl Pts',(-20.2760730898189,-20.9954310816997,
7.24902098084176));
#153178=CARTESIAN_POINT('Ctrl Pts',(-20.3421228419793,-20.9455867065661,
7.25316224442402));
#153179=CARTESIAN_POINT('Ctrl Pts',(-20.4058887674612,-20.892434299838,
7.25730350800628));
#153180=CARTESIAN_POINT('Ctrl Pts',(-20.4670153688586,-20.8362127616859,
7.26144477158854));
#153181=CARTESIAN_POINT('Ctrl Pts',(-20.5280546973635,-20.7800714932714,
7.26558012252323));
#153182=CARTESIAN_POINT('Ctrl Pts',(-20.5864618395735,-20.7208701082191,
7.26971547345792));
#153183=CARTESIAN_POINT('Ctrl Pts',(-20.6419120481562,-20.6588894564384,
7.27385082439262));
#153184=CARTESIAN_POINT('Ctrl Pts',(-20.6972986881794,-20.5969798597691,
7.27798143452815));
#153185=CARTESIAN_POINT('Ctrl Pts',(-20.7497348173452,-20.5322976752762,
7.28211204466369));
#153186=CARTESIAN_POINT('Ctrl Pts',(-20.7989315869957,-20.465161439182,
7.28624265479922));
#153187=CARTESIAN_POINT('Ctrl Pts',(-20.848098059321,-20.3980665482492,
7.29037072114094));
#153188=CARTESIAN_POINT('Ctrl Pts',(-20.8940288533086,-20.328520983131,
7.29449878748266));
#153189=CARTESIAN_POINT('Ctrl Pts',(-20.9364753744699,-20.2568763255013,
7.29862685382437));
#153190=CARTESIAN_POINT('Ctrl Pts',(-20.9789091334294,-20.1852532089438,
7.30275367899922));
#153191=CARTESIAN_POINT('Ctrl Pts',(-21.0178604599826,-20.11153265758,7.30688050417406));
#153192=CARTESIAN_POINT('Ctrl Pts',(-21.0531249145872,-20.0360939214574,
7.31100732934891));
#153193=CARTESIAN_POINT('Ctrl Pts',(-21.0883898804923,-19.9606540915461,
7.31513421435873));
#153194=CARTESIAN_POINT('Ctrl Pts',(-21.1199676712092,-19.8834964546654,
7.31926109936854));
#153195=CARTESIAN_POINT('Ctrl Pts',(-21.147701166054,-19.8050220870467,
7.32338798437836));
#153196=CARTESIAN_POINT('Ctrl Pts',(-21.175460263615,-19.7264752742866,
7.32751867920248));
#153197=CARTESIAN_POINT('Ctrl Pts',(-21.1993678247306,-19.6466097489538,
7.3316493740266));
#153198=CARTESIAN_POINT('Ctrl Pts',(-21.2193162430201,-19.5658429540041,
7.33578006885071));
#153199=CARTESIAN_POINT('Ctrl Pts',(-21.2392749611597,-19.4850344572076,
7.33991289645233));
#153200=CARTESIAN_POINT('Ctrl Pts',(-21.2552703785522,-19.4033242264923,
7.34404572405394));
#153201=CARTESIAN_POINT('Ctrl Pts',(-21.2672462583489,-19.3211387199431,
7.34817855165556));
#153202=CARTESIAN_POINT('Ctrl Pts',(-21.2792406903518,-19.2388258972814,
7.35231778154836));
#153203=CARTESIAN_POINT('Ctrl Pts',(-21.287203113202,-19.1560367972438,
7.35645701144116));
#153204=CARTESIAN_POINT('Ctrl Pts',(-21.291129302603,-19.0732011954116,
7.36059624133396));
#153205=CARTESIAN_POINT('Ctrl Pts',(-21.2930622985235,-19.0324184251309,
7.36263412429881));
#153206=CARTESIAN_POINT('Ctrl Pts',(-21.2940177418851,-18.9916243590029,
7.36467200726366));
#153207=CARTESIAN_POINT('Ctrl Pts',(-21.2939997505486,-18.9508698712832,
7.36670989022851));
#153208=CARTESIAN_POINT('Ctrl Pts',(-21.2976210191122,-18.9508682726504,
7.36670989022851));
#153209=CARTESIAN_POINT('Ctrl Pts',(-21.2979707979485,-18.88753758729,7.36987218932674));
#153210=CARTESIAN_POINT('Ctrl Pts',(-21.2671017039969,-17.9755793917529,
7.41542642398544));
#153211=CARTESIAN_POINT('Ctrl Pts',(-20.1784866426459,-16.2917839998255,
7.50337259420463));
#153212=CARTESIAN_POINT('Ctrl Pts',(-17.2790525549706,-16.2974908625944,
7.63054840088605));
#153213=CARTESIAN_POINT('Ctrl Pts',(-15.721016444231,-18.7282885581798,
7.7571898547655));
#153214=CARTESIAN_POINT('Ctrl Pts',(-16.5081486620308,-20.4743154612817,
7.84143937308446));
#153215=CARTESIAN_POINT('Ctrl Pts',(-17.1718944119077,-20.9854718354495,
7.88329695584294));
#153216=CARTESIAN_POINT('Origin',(-18.734,-18.952,-1.76670989022851));
#153217=CARTESIAN_POINT('',(-17.1744641402401,-20.9821349467765,8.74981198891561));
#153218=CARTESIAN_POINT('',(-17.1744641402401,-20.9821349467765,8.68337762424306));
#153219=CARTESIAN_POINT('',(-17.1744641402401,-20.9821349467765,-1.76670989022851));
#153220=CARTESIAN_POINT('',(-21.2939989173812,-18.9496456407966,8.23329012251171));
#153221=CARTESIAN_POINT('Ctrl Pts',(-21.2939989173812,-18.9496456407966,
8.23329012251171));
#153222=CARTESIAN_POINT('Ctrl Pts',(-21.2938985191548,-18.8404782076697,
8.23871812867059));
#153223=CARTESIAN_POINT('Ctrl Pts',(-21.2868114602984,-18.7316228556169,
8.24414613482947));
#153224=CARTESIAN_POINT('Ctrl Pts',(-21.272879163598,-18.6238345041783,
8.24957414098835));
#153225=CARTESIAN_POINT('Ctrl Pts',(-21.2596700733063,-18.5216412981934,
8.25472038679393));
#153226=CARTESIAN_POINT('Ctrl Pts',(-21.2403084403045,-18.4204066645113,
8.25986663259951));
#153227=CARTESIAN_POINT('Ctrl Pts',(-21.2149532278239,-18.3207543415199,
8.26501287840509));
#153228=CARTESIAN_POINT('Ctrl Pts',(-21.1943358111288,-18.2397227402535,
8.26919751279814));
#153229=CARTESIAN_POINT('Ctrl Pts',(-21.1697059337058,-18.1595514977396,
8.27338214719119));
#153230=CARTESIAN_POINT('Ctrl Pts',(-21.1411517779373,-18.0806675043514,
8.27756678158424));
#153231=CARTESIAN_POINT('Ctrl Pts',(-21.1126382654753,-18.001895792564,
8.28174545966817));
#153232=CARTESIAN_POINT('Ctrl Pts',(-21.0802117249138,-17.9244081193636,
8.28592413775211));
#153233=CARTESIAN_POINT('Ctrl Pts',(-21.0440107968602,-17.8486187792112,
8.29010281583605));
#153234=CARTESIAN_POINT('Ctrl Pts',(-21.0071609931883,-17.7714709696052,
8.29435639372149));
#153235=CARTESIAN_POINT('Ctrl Pts',(-20.9664002781983,-17.6960834444032,
8.29860997160693));
#153236=CARTESIAN_POINT('Ctrl Pts',(-20.9219272181895,-17.6228745401937,
8.30286354949236));
#153237=CARTESIAN_POINT('Ctrl Pts',(-20.8783163552311,-17.5510849334477,
8.30703466347032));
#153238=CARTESIAN_POINT('Ctrl Pts',(-20.8311360546879,-17.481390639162,
8.31120577744827));
#153239=CARTESIAN_POINT('Ctrl Pts',(-20.7806202689679,-17.4141620778997,
8.31537689142622));
#153240=CARTESIAN_POINT('Ctrl Pts',(-20.7301214343076,-17.3469560758303,
8.31954660574659));
#153241=CARTESIAN_POINT('Ctrl Pts',(-20.6762896134472,-17.282214531026,
8.32371632006697));
#153242=CARTESIAN_POINT('Ctrl Pts',(-20.6194012584855,-17.2202777086088,
8.32788603438735));
#153243=CARTESIAN_POINT('Ctrl Pts',(-20.5625149278557,-17.1583430901695,
8.33205560033139));
#153244=CARTESIAN_POINT('Ctrl Pts',(-20.5025725911954,-17.0992133339121,
8.33622516627543));
#153245=CARTESIAN_POINT('Ctrl Pts',(-20.4398891227941,-17.0431934878745,
8.34039473221948));
#153246=CARTESIAN_POINT('Ctrl Pts',(-20.3750017809722,-16.9852040531582,
8.3447108949584));
#153247=CARTESIAN_POINT('Ctrl Pts',(-20.307177357872,-16.9305476379183,
8.34902705769732));
#153248=CARTESIAN_POINT('Ctrl Pts',(-20.2368028123897,-16.8795175013831,
8.35334322043624));
#153249=CARTESIAN_POINT('Ctrl Pts',(-20.1687207103245,-16.830149666178,
8.35751878462792));
#153250=CARTESIAN_POINT('Ctrl Pts',(-20.0982524952704,-16.7841757035314,
8.3616943488196));
#153251=CARTESIAN_POINT('Ctrl Pts',(-20.0257768405865,-16.7418161628216,
8.36586991301128));
#153252=CARTESIAN_POINT('Ctrl Pts',(-19.9496406128789,-16.6973171424108,
8.37025637502383));
#153253=CARTESIAN_POINT('Ctrl Pts',(-19.8712893431907,-16.656807536765,
8.37464283703637));
#153254=CARTESIAN_POINT('Ctrl Pts',(-19.7911876038235,-16.6204866780732,
8.37902929904891));
#153255=CARTESIAN_POINT('Ctrl Pts',(-19.7110858644562,-16.5841658193814,
8.38341576106145));
#153256=CARTESIAN_POINT('Ctrl Pts',(-19.6292342232968,-16.5520338488593,
8.38780222307399));
#153257=CARTESIAN_POINT('Ctrl Pts',(-19.5461152252309,-16.524229652346,
8.39218868508653));
#153258=CARTESIAN_POINT('Ctrl Pts',(-19.466820655478,-16.49770476813,8.39637331947958));
#153259=CARTESIAN_POINT('Ctrl Pts',(-19.3860776423915,-16.4750194242752,
8.40055795387263));
#153260=CARTESIAN_POINT('Ctrl Pts',(-19.3042928646695,-16.4563305410157,
8.40474258826568));
#153261=CARTESIAN_POINT('Ctrl Pts',(-19.2226244974556,-16.4376682590682,
8.40892126634962));
#153262=CARTESIAN_POINT('Ctrl Pts',(-19.1399177555962,-16.4229912402357,
8.41309994443357));
#153263=CARTESIAN_POINT('Ctrl Pts',(-19.0565960387005,-16.4124071594417,
8.41727862251751));
#153264=CARTESIAN_POINT('Ctrl Pts',(-18.9717808399117,-16.4016333666062,
8.42153220040295));
#153265=CARTESIAN_POINT('Ctrl Pts',(-18.8863288596153,-16.3951008398354,
8.42578577828838));
#153266=CARTESIAN_POINT('Ctrl Pts',(-18.8006993328509,-16.3928690539566,
8.43003935617382));
#153267=CARTESIAN_POINT('Ctrl Pts',(-18.7167299015551,-16.3906805356019,
8.43421047015177));
#153268=CARTESIAN_POINT('Ctrl Pts',(-18.6325902275832,-16.3926275022743,
8.43838158412972));
#153269=CARTESIAN_POINT('Ctrl Pts',(-18.5487184100095,-16.3987137386477,
8.44255269810768));
#153270=CARTESIAN_POINT('Ctrl Pts',(-18.4648747364341,-16.4047979327256,
8.44672241242805));
#153271=CARTESIAN_POINT('Ctrl Pts',(-18.3812991991949,-16.4150186047169,
8.45089212674842));
#153272=CARTESIAN_POINT('Ctrl Pts',(-18.2984275456889,-16.4293274812125,
8.4550618410688));
#153273=CARTESIAN_POINT('Ctrl Pts',(-18.2155588411121,-16.443635848537,
8.45923140701284));
#153274=CARTESIAN_POINT('Ctrl Pts',(-18.1333944236484,-16.4620320520103,
8.46340097295688));
#153275=CARTESIAN_POINT('Ctrl Pts',(-18.0523612259041,-16.4844164489021,
8.46757053890092));
#153276=CARTESIAN_POINT('Ctrl Pts',(-17.9684790008923,-16.5075878535745,
8.47188670163984));
#153277=CARTESIAN_POINT('Ctrl Pts',(-17.8858095314086,-16.5350329790257,
8.47620286437876));
#153278=CARTESIAN_POINT('Ctrl Pts',(-17.8048088555659,-16.5665851897196,
8.48051902711769));
#153279=CARTESIAN_POINT('Ctrl Pts',(-17.7264467682191,-16.5971095904688,
8.48469459130937));
#153280=CARTESIAN_POINT('Ctrl Pts',(-17.6496468328973,-16.631477373477,
8.48887015550105));
#153281=CARTESIAN_POINT('Ctrl Pts',(-17.5747994654321,-16.6694895135712,
8.49304571969273));
#153282=CARTESIAN_POINT('Ctrl Pts',(-17.4961717353689,-16.7094215564963,
8.49743218170527));
#153283=CARTESIAN_POINT('Ctrl Pts',(-17.4196995115721,-16.7533754937362,
8.50181864371781));
#153284=CARTESIAN_POINT('Ctrl Pts',(-17.3458018650429,-16.8010685882387,
8.50620510573035));
#153285=CARTESIAN_POINT('Ctrl Pts',(-17.2719042185137,-16.8487616827411,
8.51059156774289));
#153286=CARTESIAN_POINT('Ctrl Pts',(-17.2005815753788,-16.9001935334405,
8.51497802975543));
#153287=CARTESIAN_POINT('Ctrl Pts',(-17.1322119090441,-16.9550335727229,
8.51936449176797));
#153288=CARTESIAN_POINT('Ctrl Pts',(-17.0669880324055,-17.0073503405056,
8.52354912616102));
#153289=CARTESIAN_POINT('Ctrl Pts',(-17.0042085866858,-17.0629632902855,
8.52773376055407));
#153290=CARTESIAN_POINT('Ctrl Pts',(-16.9442256444345,-17.1216154075823,
8.53191839494712));
#153291=CARTESIAN_POINT('Ctrl Pts',(-16.8843280804771,-17.1801840408498,
8.53609707303106));
#153292=CARTESIAN_POINT('Ctrl Pts',(-16.8272194396165,-17.2417829302056,
8.540275751115));
#153293=CARTESIAN_POINT('Ctrl Pts',(-16.7732194376016,-17.3061143459765,
8.54445442919894));
#153294=CARTESIAN_POINT('Ctrl Pts',(-16.7182515243596,-17.3715988561409,
8.54870800708438));
#153295=CARTESIAN_POINT('Ctrl Pts',(-16.6665051669308,-17.4399145156592,
8.55296158496982));
#153296=CARTESIAN_POINT('Ctrl Pts',(-16.6182789494493,-17.5107073731346,
8.55721516285525));
#153297=CARTESIAN_POINT('Ctrl Pts',(-16.5709876912994,-17.5801277729269,
8.5613862768332));
#153298=CARTESIAN_POINT('Ctrl Pts',(-16.5270815724709,-17.6519297794778,
8.56555739081116));
#153299=CARTESIAN_POINT('Ctrl Pts',(-16.4868009099952,-17.7257470693687,
8.56972850478911));
#153300=CARTESIAN_POINT('Ctrl Pts',(-16.4465337640849,-17.7995395891551,
8.57389821910948));
#153301=CARTESIAN_POINT('Ctrl Pts',(-16.409889878601,-17.8753456457563,
8.57806793342985));
#153302=CARTESIAN_POINT('Ctrl Pts',(-16.3770645250475,-17.952772715089,
8.58223764775022));
#153303=CARTESIAN_POINT('Ctrl Pts',(-16.344240339561,-18.0301970292344,
8.58640721369426));
#153304=CARTESIAN_POINT('Ctrl Pts',(-16.315234594618,-18.1092418175489,
8.59057677963831));
#153305=CARTESIAN_POINT('Ctrl Pts',(-16.2901945969736,-18.1894941625542,
8.59474634558235));
#153306=CARTESIAN_POINT('Ctrl Pts',(-16.2642742239021,-18.2725680810079,
8.59906250832127));
#153307=CARTESIAN_POINT('Ctrl Pts',(-16.2426038152403,-18.3569355479853,
8.60337867106019));
#153308=CARTESIAN_POINT('Ctrl Pts',(-16.2252901016539,-18.4421229109477,
8.60769483379911));
#153309=CARTESIAN_POINT('Ctrl Pts',(-16.2085403804665,-18.5245353045217,
8.61187039799079));
#153310=CARTESIAN_POINT('Ctrl Pts',(-16.1958678987932,-18.6077145253799,
8.61604596218247));
#153311=CARTESIAN_POINT('Ctrl Pts',(-16.1873166326445,-18.6912245670412,
8.62022152637415));
#153312=CARTESIAN_POINT('Ctrl Pts',(-16.1783334623714,-18.7789525023805,
8.62460798838669));
#153313=CARTESIAN_POINT('Ctrl Pts',(-16.1738988033979,-18.8670449731774,
8.62899445039923));
#153314=CARTESIAN_POINT('Ctrl Pts',(-16.1740017537922,-18.9549965668354,
8.63338091241177));
#153315=CARTESIAN_POINT('Ctrl Pts',(-16.1741047041864,-19.0429481604934,
8.63776737442431));
#153316=CARTESIAN_POINT('Ctrl Pts',(-16.1787451573697,-19.1307583016182,
8.64215383643685));
#153317=CARTESIAN_POINT('Ctrl Pts',(-16.1878497481281,-19.2179302444114,
8.64654029844939));
#153318=CARTESIAN_POINT('Ctrl Pts',(-16.1967810774084,-19.303443294448,
8.65084328555215));
#153319=CARTESIAN_POINT('Ctrl Pts',(-16.210042254892,-19.3886695640475,
8.65514627265491));
#153320=CARTESIAN_POINT('Ctrl Pts',(-16.2276047119207,-19.4731359322611,
8.65944925975767));
#153321=CARTESIAN_POINT('Ctrl Pts',(-16.2446561825664,-19.5551447192891,
8.66362704981018));
#153322=CARTESIAN_POINT('Ctrl Pts',(-16.2657620068644,-19.6364367189553,
8.66780483986269));
#153323=CARTESIAN_POINT('Ctrl Pts',(-16.2908434896405,-19.7165824127508,
8.67198262991519));
#153324=CARTESIAN_POINT('Ctrl Pts',(-16.3159003340244,-19.7966493767103,
8.67615631598269));
#153325=CARTESIAN_POINT('Ctrl Pts',(-16.3449249457181,-19.8755718341914,
8.68033000205019));
#153326=CARTESIAN_POINT('Ctrl Pts',(-16.3777879099992,-19.9529318592862,
8.68450368811769));
#153327=CARTESIAN_POINT('Ctrl Pts',(-16.4106284513386,-20.0302391003617,
8.68867452641044));
#153328=CARTESIAN_POINT('Ctrl Pts',(-16.4473019635812,-20.1059856045522,
8.6928453647032));
#153329=CARTESIAN_POINT('Ctrl Pts',(-16.4876301097207,-20.1797712800218,
8.69701620299595));
#153330=CARTESIAN_POINT('Ctrl Pts',(-16.5279428373367,-20.2535287452641,
8.70118544666623));
#153331=CARTESIAN_POINT('Ctrl Pts',(-16.5719072007185,-20.325326468996,
8.70535469033651));
#153332=CARTESIAN_POINT('Ctrl Pts',(-16.6192985221864,-20.3947881548353,
8.70952393400679));
#153333=CARTESIAN_POINT('Ctrl Pts',(-16.6667008411468,-20.4642659597516,
8.71369414517964));
#153334=CARTESIAN_POINT('Ctrl Pts',(-16.7175314520026,-20.5314062606125,
8.7178643563525));
#153335=CARTESIAN_POINT('Ctrl Pts',(-16.7715224002379,-20.5958618161002,
8.72203456752536));
#153336=CARTESIAN_POINT('Ctrl Pts',(-16.8255216898818,-20.6603273297408,
8.72620542298094));
#153337=CARTESIAN_POINT('Ctrl Pts',(-16.8826819840771,-20.7221069276297,
8.73037627843651));
#153338=CARTESIAN_POINT('Ctrl Pts',(-16.9426963304669,-20.780887958164,
8.73454713389209));
#153339=CARTESIAN_POINT('Ctrl Pts',(-17.0027604653468,-20.8397177540175,
8.73872144953024));
#153340=CARTESIAN_POINT('Ctrl Pts',(-17.0656830383974,-20.8955437075325,
8.74289576516841));
#153341=CARTESIAN_POINT('Ctrl Pts',(-17.1311223583306,-20.9480919983398,
8.74707008080657));
#153342=CARTESIAN_POINT('Ctrl Pts',(-17.145450343844,-20.9595974838829,
8.74798405017625));
#153343=CARTESIAN_POINT('Ctrl Pts',(-17.1598988634156,-20.970946000174,
8.74889801954593));
#153344=CARTESIAN_POINT('Ctrl Pts',(-17.1744641402401,-20.9821349467765,
8.74981198891562));
#153345=CARTESIAN_POINT('Ctrl Pts',(-17.1770150605606,-20.9788230109682,
7.94987221524758));
#153346=CARTESIAN_POINT('Ctrl Pts',(-17.501044950009,-21.2283579020811,
7.9701352318458));
#153347=CARTESIAN_POINT('Ctrl Pts',(-18.677462676132,-21.7718986662915,
8.03279018400449));
#153348=CARTESIAN_POINT('Ctrl Pts',(-20.7208249517526,-21.0909115417432,
8.12726281551247));
#153349=CARTESIAN_POINT('Ctrl Pts',(-21.2877697529773,-19.5894613481947,
8.20147243042223));
#153350=CARTESIAN_POINT('Ctrl Pts',(-21.2935816048406,-18.9496462807751,
8.23329010977151));
#153351=CARTESIAN_POINT('',(-21.2939989424941,-18.9543268925436,8.16670989022853));
#153352=CARTESIAN_POINT('Ctrl Pts',(-17.1718944119077,-20.9854718354495,
7.88329695584294));
#153353=CARTESIAN_POINT('Ctrl Pts',(-17.1803677727156,-20.9919972442953,
7.88383130864493));
#153354=CARTESIAN_POINT('Ctrl Pts',(-17.864630092765,-21.5115395255608,
7.92675759700741));
#153355=CARTESIAN_POINT('Ctrl Pts',(-19.7898862882482,-21.7889693291709,
8.01207582093036));
#153356=CARTESIAN_POINT('Ctrl Pts',(-21.1940976605954,-20.1719438373811,
8.10601244625689));
#153357=CARTESIAN_POINT('Ctrl Pts',(-21.2961551338926,-19.1382186499617,
8.15755713602294));
#153358=CARTESIAN_POINT('Ctrl Pts',(-21.2944496155086,-18.9543273021797,
8.16670989022852));
#153359=CARTESIAN_POINT('Ctrl Pts',(-21.2939989424941,-18.9543268925437,
8.16670989022852));
#153360=CARTESIAN_POINT('Ctrl Pts',(-21.2940748047761,-18.8708647825268,
8.17086478789788));
#153361=CARTESIAN_POINT('Ctrl Pts',(-21.2900646933588,-18.7872780169979,
8.17501968556725));
#153362=CARTESIAN_POINT('Ctrl Pts',(-21.2819596922617,-18.7040052286649,
8.17917458323661));
#153363=CARTESIAN_POINT('Ctrl Pts',(-21.2739328413916,-18.621535375116,
8.18328941845664));
#153364=CARTESIAN_POINT('Ctrl Pts',(-21.2618897634889,-18.539373952273,
8.18740425367668));
#153365=CARTESIAN_POINT('Ctrl Pts',(-21.2458740550218,-18.4579466307083,
8.19151908889671));
#153366=CARTESIAN_POINT('Ctrl Pts',(-21.2298653109089,-18.3765547174254,
8.19563213480031));
#153367=CARTESIAN_POINT('Ctrl Pts',(-21.2098874553344,-18.2958967363637,
8.1997451807039));
#153368=CARTESIAN_POINT('Ctrl Pts',(-21.1860355605651,-18.2163903142807,
8.20385822660749));
#153369=CARTESIAN_POINT('Ctrl Pts',(-21.1621864189584,-18.1368930694186,
8.20797079775283));
#153370=CARTESIAN_POINT('Ctrl Pts',(-21.1344642632166,-18.0585475732026,
8.21208336889816));
#153371=CARTESIAN_POINT('Ctrl Pts',(-21.1030141994635,-17.9817568744174,
8.2161959400435));
#153372=CARTESIAN_POINT('Ctrl Pts',(-21.0710029255601,-17.9035958852586,
8.22038189789764));
#153373=CARTESIAN_POINT('Ctrl Pts',(-21.035129571801,-17.8270462022335,
8.22456785575179));
#153374=CARTESIAN_POINT('Ctrl Pts',(-20.9955977974881,-17.7525103575283,
8.22875381360593));
#153375=CARTESIAN_POINT('Ctrl Pts',(-20.9567081892511,-17.6791852955855,
8.23287177349703));
#153376=CARTESIAN_POINT('Ctrl Pts',(-20.9142784405326,-17.6078095092631,
8.23698973338812));
#153377=CARTESIAN_POINT('Ctrl Pts',(-20.8685472200434,-17.5387384653204,
8.24110769327921));
#153378=CARTESIAN_POINT('Ctrl Pts',(-20.8216832918823,-17.4679566141755,
8.24532765011488));
#153379=CARTESIAN_POINT('Ctrl Pts',(-20.7713524862055,-17.399595623106,
8.24954760695055));
#153380=CARTESIAN_POINT('Ctrl Pts',(-20.7178552814754,-17.3340017854886,
8.25376756378622));
#153381=CARTESIAN_POINT('Ctrl Pts',(-20.6643580767453,-17.2684079478711,
8.25798752062189));
#153382=CARTESIAN_POINT('Ctrl Pts',(-20.6076948817587,-17.2055816046285,
8.26220747745756));
#153383=CARTESIAN_POINT('Ctrl Pts',(-20.5482046419776,-17.1458268308308,
8.26642743429323));
#153384=CARTESIAN_POINT('Ctrl Pts',(-20.4892123552949,-17.0865722243692,
8.27061206868627));
#153385=CARTESIAN_POINT('Ctrl Pts',(-20.427204219073,-17.0301005497847,
8.27479670307932));
#153386=CARTESIAN_POINT('Ctrl Pts',(-20.3624734272386,-16.9767343731088,
8.27898133747237));
#153387=CARTESIAN_POINT('Ctrl Pts',(-20.2978347716741,-16.9234441565799,
8.28316001555632));
#153388=CARTESIAN_POINT('Ctrl Pts',(-20.230481510108,-16.8732509480032,
8.28733869364026));
#153389=CARTESIAN_POINT('Ctrl Pts',(-20.1607438576395,-16.8264407877718,
8.29151737172421));
#153390=CARTESIAN_POINT('Ctrl Pts',(-20.08975620787,-16.7787915890602,8.29577094960965));
#153391=CARTESIAN_POINT('Ctrl Pts',(-20.0162981861697,-16.7346482555833,
8.30002452749508));
#153392=CARTESIAN_POINT('Ctrl Pts',(-19.9407536469187,-16.6942698045053,
8.30427810538052));
#153393=CARTESIAN_POINT('Ctrl Pts',(-19.8666736859741,-16.6546741684936,
8.30844921935847));
#153394=CARTESIAN_POINT('Ctrl Pts',(-19.7905878123475,-16.6186989652308,
8.31262033333642));
#153395=CARTESIAN_POINT('Ctrl Pts',(-19.7128859499199,-16.5865439557985,
8.31679144731437));
#153396=CARTESIAN_POINT('Ctrl Pts',(-19.6352101611027,-16.5543997362902,
8.32096116163474));
#153397=CARTESIAN_POINT('Ctrl Pts',(-19.5559198851422,-16.5260733404925,
8.32513087595511));
#153398=CARTESIAN_POINT('Ctrl Pts',(-19.4754262787741,-16.5017169401999,
8.32930059027548));
#153399=CARTESIAN_POINT('Ctrl Pts',(-19.3949355367137,-16.4773614066125,
8.33347015621953));
#153400=CARTESIAN_POINT('Ctrl Pts',(-19.3132419899457,-16.4569757200691,
8.33763972216358));
#153401=CARTESIAN_POINT('Ctrl Pts',(-19.230771941892,-16.4406621816751,
8.34180928810762));
#153402=CARTESIAN_POINT('Ctrl Pts',(-19.1454023486867,-16.4237750793961,
8.34612545084654));
#153403=CARTESIAN_POINT('Ctrl Pts',(-19.0592011520725,-16.4112519089494,
8.35044161358546));
#153404=CARTESIAN_POINT('Ctrl Pts',(-18.9726507026517,-16.4031481325656,
8.35475777632438));
#153405=CARTESIAN_POINT('Ctrl Pts',(-18.8889196250172,-16.3953083358451,
8.35893334051606));
#153406=CARTESIAN_POINT('Ctrl Pts',(-18.8048621716341,-16.3916044048151,
8.36310890470774));
#153407=CARTESIAN_POINT('Ctrl Pts',(-18.7209165514642,-16.392033433153,
8.36728446889942));
#153408=CARTESIAN_POINT('Ctrl Pts',(-18.6327310375814,-16.3924841306923,
8.37167093091196));
#153409=CARTESIAN_POINT('Ctrl Pts',(-18.544669534143,-16.3974962383813,
8.3760573929245));
#153410=CARTESIAN_POINT('Ctrl Pts',(-18.4572333890563,-16.4070048638422,
8.38044385493705));
#153411=CARTESIAN_POINT('Ctrl Pts',(-18.3697972439697,-16.4165134893032,
8.38483031694959));
#153412=CARTESIAN_POINT('Ctrl Pts',(-18.2829870179305,-16.4305184650313,
8.38921677896213));
#153413=CARTESIAN_POINT('Ctrl Pts',(-18.1972887614196,-16.4488937205182,
8.39360324097467));
#153414=CARTESIAN_POINT('Ctrl Pts',(-18.115533608726,-16.4664235032614,
8.39778787536772));
#153415=CARTESIAN_POINT('Ctrl Pts',(-18.0344860391771,-16.4879954864412,
8.40197250976076));
#153416=CARTESIAN_POINT('Ctrl Pts',(-17.9545759800698,-16.513537739239,
8.40615714415381));
#153417=CARTESIAN_POINT('Ctrl Pts',(-17.8747796630406,-16.5390436358014,
8.41033582223776));
#153418=CARTESIAN_POINT('Ctrl Pts',(-17.796118074845,-16.5685084380807,
8.4145145003217));
#153419=CARTESIAN_POINT('Ctrl Pts',(-17.7190104693569,-16.6018093156757,
8.41869317840565));
#153420=CARTESIAN_POINT('Ctrl Pts',(-17.6405207654567,-16.6357070875686,
8.42294675629108));
#153421=CARTESIAN_POINT('Ctrl Pts',(-17.5636417739317,-16.673579709668,
8.42720033417652));
#153422=CARTESIAN_POINT('Ctrl Pts',(-17.4887990603226,-16.715244622265,
8.43145391206195));
#153423=CARTESIAN_POINT('Ctrl Pts',(-17.4154073187602,-16.7561017792289,
8.43562502603991));
#153424=CARTESIAN_POINT('Ctrl Pts',(-17.3439740257042,-16.8006052628959,
8.43979614001786));
#153425=CARTESIAN_POINT('Ctrl Pts',(-17.2748782070124,-16.8485353358735,
8.44396725399581));
#153426=CARTESIAN_POINT('Ctrl Pts',(-17.20580557409,-16.8964493254522,8.44813696831618));
#153427=CARTESIAN_POINT('Ctrl Pts',(-17.1390692354551,-16.9477873587841,
8.45230668263656));
#153428=CARTESIAN_POINT('Ctrl Pts',(-17.0750196948478,-17.0022860858277,
8.45647639695693));
#153429=CARTESIAN_POINT('Ctrl Pts',(-17.010972433398,-17.0567828735727,
8.46064596290098));
#153430=CARTESIAN_POINT('Ctrl Pts',(-16.949612129695,-17.1144398326397,
8.46481552884502));
#153431=CARTESIAN_POINT('Ctrl Pts',(-16.8912555527359,-17.1749538829628,
8.46898509478907));
#153432=CARTESIAN_POINT('Ctrl Pts',(-16.8308472305215,-17.237595532643,
8.47330125752799));
#153433=CARTESIAN_POINT('Ctrl Pts',(-16.7736581532182,-17.3032985427183,
8.47761742026691));
#153434=CARTESIAN_POINT('Ctrl Pts',(-16.7199960430175,-17.3716873533194,
8.48193358300583));
#153435=CARTESIAN_POINT('Ctrl Pts',(-16.6680819704122,-17.4378484056084,
8.48610914719751));
#153436=CARTESIAN_POINT('Ctrl Pts',(-16.6194688453352,-17.5065225539072,
8.49028471138918));
#153437=CARTESIAN_POINT('Ctrl Pts',(-16.5743914182288,-17.5773397606898,
8.49446027558086));
#153438=CARTESIAN_POINT('Ctrl Pts',(-16.5270372374408,-17.6517337762351,
8.4988467375934));
#153439=CARTESIAN_POINT('Ctrl Pts',(-16.4835856052312,-17.7284925234216,
8.50323319960595));
#153440=CARTESIAN_POINT('Ctrl Pts',(-16.4442533274935,-17.8071593229862,
8.50761966161849));
#153441=CARTESIAN_POINT('Ctrl Pts',(-16.4049210497558,-17.8858261225507,
8.51200612363103));
#153442=CARTESIAN_POINT('Ctrl Pts',(-16.3697082891389,-17.9664004123698,
8.51639258564357));
#153443=CARTESIAN_POINT('Ctrl Pts',(-16.3387721302027,-18.0484052613331,
8.52077904765611));
#153444=CARTESIAN_POINT('Ctrl Pts',(-16.3092593897976,-18.1266369456353,
8.52496368204916));
#153445=CARTESIAN_POINT('Ctrl Pts',(-16.2835285016033,-18.2064616309202,
8.5291483164422));
#153446=CARTESIAN_POINT('Ctrl Pts',(-16.2617516946765,-18.2874788815808,
8.53333295083525));
#153447=CARTESIAN_POINT('Ctrl Pts',(-16.240005884339,-18.3683808142128,
8.53751162891919));
#153448=CARTESIAN_POINT('Ctrl Pts',(-16.2222030943946,-18.4504715000485,
8.54169030700313));
#153449=CARTESIAN_POINT('Ctrl Pts',(-16.2084669780844,-18.5333319271618,
8.54586898508706));
#153450=CARTESIAN_POINT('Ctrl Pts',(-16.1944846517614,-18.6176775678805,
8.5501225629725));
#153451=CARTESIAN_POINT('Ctrl Pts',(-16.1847163934876,-18.7028203654201,
8.55437614085793));
#153452=CARTESIAN_POINT('Ctrl Pts',(-16.179239049994,-18.7883036704004,
8.55862971874337));
#153453=CARTESIAN_POINT('Ctrl Pts',(-16.1738678954921,-18.8721297147068,
8.56280083272133));
#153454=CARTESIAN_POINT('Ctrl Pts',(-16.1726227957354,-18.9562827012368,
8.56697194669928));
#153455=CARTESIAN_POINT('Ctrl Pts',(-16.1755241458591,-19.0403249895433,
8.57114306067723));
#153456=CARTESIAN_POINT('Ctrl Pts',(-16.1784245224067,-19.1243390766483,
8.57531277499761));
#153457=CARTESIAN_POINT('Ctrl Pts',(-16.1854685696706,-19.2082420799255,
8.57948248931799));
#153458=CARTESIAN_POINT('Ctrl Pts',(-16.1966245729686,-19.2915967348153,
8.58365220363836));
#153459=CARTESIAN_POINT('Ctrl Pts',(-16.2077801792881,-19.3749484235886,
8.5878217695824));
#153460=CARTESIAN_POINT('Ctrl Pts',(-16.2230473888476,-19.4577513469163,
8.59199133552644));
#153461=CARTESIAN_POINT('Ctrl Pts',(-16.2423428203252,-19.5395751007105,
8.59616090147048));
#153462=CARTESIAN_POINT('Ctrl Pts',(-16.2623166553701,-19.6242756767476,
8.6004770642094));
#153463=CARTESIAN_POINT('Ctrl Pts',(-16.286607126249,-19.7079264335896,
8.60479322694832));
#153464=CARTESIAN_POINT('Ctrl Pts',(-16.3150650107314,-19.7900653421374,
8.60910938968724));
#153465=CARTESIAN_POINT('Ctrl Pts',(-16.3425958826199,-19.8695285843788,
8.61328495387892));
#153466=CARTESIAN_POINT('Ctrl Pts',(-16.3740266108363,-19.9475765433407,
8.6174605180706));
#153467=CARTESIAN_POINT('Ctrl Pts',(-16.4091731183428,-20.0238115367565,
8.62163608226228));
#153468=CARTESIAN_POINT('Ctrl Pts',(-16.4460947923907,-20.1038969784582,
8.62602254427482));
#153469=CARTESIAN_POINT('Ctrl Pts',(-16.4871172070498,-20.1819809787839,
8.63040900628736));
#153470=CARTESIAN_POINT('Ctrl Pts',(-16.5319737202489,-20.2576340464639,
8.63479546829991));
#153471=CARTESIAN_POINT('Ctrl Pts',(-16.576830233448,-20.3332871141439,
8.63918193031245));
#153472=CARTESIAN_POINT('Ctrl Pts',(-16.625520460569,-20.4065088081493,
8.64356839232499));
#153473=CARTESIAN_POINT('Ctrl Pts',(-16.677728404917,-20.4769088914603,
8.64795485433753));
#153474=CARTESIAN_POINT('Ctrl Pts',(-16.7275305669034,-20.5440648846084,
8.65213918479575));
#153475=CARTESIAN_POINT('Ctrl Pts',(-16.7807187430381,-20.6089035367426,
8.65632351525396));
#153476=CARTESIAN_POINT('Ctrl Pts',(-16.8370495093351,-20.671063360079,
8.66050784571218));
#153477=CARTESIAN_POINT('Ctrl Pts',(-16.8932939076475,-20.7331278781494,
8.6646857606321));
#153478=CARTESIAN_POINT('Ctrl Pts',(-16.9526710148719,-20.7925213917371,
8.66886367555201));
#153479=CARTESIAN_POINT('Ctrl Pts',(-17.0148956024723,-20.8489133007075,
8.67304159047192));
#153480=CARTESIAN_POINT('Ctrl Pts',(-17.0662095115363,-20.8954172535731,
8.6764869350623));
#153481=CARTESIAN_POINT('Ctrl Pts',(-17.1194590131858,-20.9398803822471,
8.67993227965268));
#153482=CARTESIAN_POINT('Ctrl Pts',(-17.1744641402401,-20.9821349467765,
8.68337762424306));
#153483=CARTESIAN_POINT('Origin',(-18.734,-18.952,-1.76670989022851));
#153484=CARTESIAN_POINT('',(-17.1725833834245,-20.9846205132764,9.54996331522893));
#153485=CARTESIAN_POINT('',(-17.1744641402401,-20.9821349467765,9.48328065029978));
#153486=CARTESIAN_POINT('',(-17.1744641402401,-20.9821349467765,-1.76670989022851));
#153487=CARTESIAN_POINT('',(-21.294330140624,-18.9526425111494,9.03329016589256));
#153488=CARTESIAN_POINT('Ctrl Pts',(-21.2980343851841,-18.9526308401995,
9.03329079542781));
#153489=CARTESIAN_POINT('Ctrl Pts',(-21.295285921847,-18.1388728971705,
9.07394170534359));
#153490=CARTESIAN_POINT('Ctrl Pts',(-20.4360628655086,-16.4715240736058,
9.15698455081984));
#153491=CARTESIAN_POINT('Ctrl Pts',(-17.5947352967179,-16.1474738554406,
9.28241933185657));
#153492=CARTESIAN_POINT('Ctrl Pts',(-15.7591749622877,-18.3919045129074,
9.40959513853801));
#153493=CARTESIAN_POINT('Ctrl Pts',(-16.3858469674303,-20.326135493453,
9.49877646632879));
#153494=CARTESIAN_POINT('Ctrl Pts',(-17.1023021555805,-20.9314719346189,
9.5455658585591));
#153495=CARTESIAN_POINT('Ctrl Pts',(-17.1725833834245,-20.9846205132764,
9.54996331522893));
#153496=CARTESIAN_POINT('Ctrl Pts',(-17.1744641402401,-20.9821349467765,
8.74981198891562));
#153497=CARTESIAN_POINT('Ctrl Pts',(-17.2411337728998,-21.0333501051849,
8.7539955003499));
#153498=CARTESIAN_POINT('Ctrl Pts',(-17.3102516250714,-21.0812183482621,
8.75817901178418));
#153499=CARTESIAN_POINT('Ctrl Pts',(-17.3814397288989,-21.1255180498535,
8.76236252321847));
#153500=CARTESIAN_POINT('Ctrl Pts',(-17.4458385782616,-21.1655928608993,
8.76614705052259));
#153501=CARTESIAN_POINT('Ctrl Pts',(-17.5119310604356,-21.202747812138,
8.76993157782671));
#153502=CARTESIAN_POINT('Ctrl Pts',(-17.5794224113972,-21.2368524223451,
8.77371610513083));
#153503=CARTESIAN_POINT('Ctrl Pts',(-17.6540490703618,-21.2745626337838,
8.77790073952388));
#153504=CARTESIAN_POINT('Ctrl Pts',(-17.7306640561251,-21.3086830520783,
8.78208537391693));
#153505=CARTESIAN_POINT('Ctrl Pts',(-17.8088876493305,-21.3389996101045,
8.78627000830998));
#153506=CARTESIAN_POINT('Ctrl Pts',(-17.8869999009332,-21.3692730162627,
8.79044868639392));
#153507=CARTESIAN_POINT('Ctrl Pts',(-17.9667157867297,-21.3957531518832,
8.79462736447786));
#153508=CARTESIAN_POINT('Ctrl Pts',(-18.0476319224909,-21.4182722603509,
8.79880604256181));
#153509=CARTESIAN_POINT('Ctrl Pts',(-18.1299984218321,-21.4411950076538,
8.80305962044724));
#153510=CARTESIAN_POINT('Ctrl Pts',(-18.213608193011,-21.4600131107992,
8.80731319833268));
#153511=CARTESIAN_POINT('Ctrl Pts',(-18.2980154243377,-21.4746013259698,
8.81156677621811));
#153512=CARTESIAN_POINT('Ctrl Pts',(-18.380786256778,-21.4889067201227,
8.81573789019606));
#153513=CARTESIAN_POINT('Ctrl Pts',(-18.4643234304655,-21.4991446900207,
8.81990900417402));
#153514=CARTESIAN_POINT('Ctrl Pts',(-18.5481939962223,-21.5052481526401,
8.82408011815197));
#153515=CARTESIAN_POINT('Ctrl Pts',(-18.6320364184008,-21.5113495671838,
8.82824983247234));
#153516=CARTESIAN_POINT('Ctrl Pts',(-18.7162115520294,-21.5133191964338,
8.83241954679272));
#153517=CARTESIAN_POINT('Ctrl Pts',(-18.8002812486104,-21.5111418085137,
8.83658926111309));
#153518=CARTESIAN_POINT('Ctrl Pts',(-18.8843479536309,-21.5089644980744,
8.84075882705713));
#153519=CARTESIAN_POINT('Ctrl Pts',(-18.9683087692068,-21.502640476632,
8.84492839300118));
#153520=CARTESIAN_POINT('Ctrl Pts',(-19.0517268423097,-21.4922066163357,
8.84909795894522));
#153521=CARTESIAN_POINT('Ctrl Pts',(-19.1380777919556,-21.481405914383,
8.85341412168414));
#153522=CARTESIAN_POINT('Ctrl Pts',(-19.2238466000237,-21.4662010579768,
8.85773028442306));
#153523=CARTESIAN_POINT('Ctrl Pts',(-19.3085579282896,-21.4466910003124,
8.86204644716198));
#153524=CARTESIAN_POINT('Ctrl Pts',(-19.3905097939472,-21.4278164807243,
8.86622201135366));
#153525=CARTESIAN_POINT('Ctrl Pts',(-19.4714715762059,-21.404913110059,
8.87039757554534));
#153526=CARTESIAN_POINT('Ctrl Pts',(-19.551028186959,-21.3781213781908,
8.87457313973702));
#153527=CARTESIAN_POINT('Ctrl Pts',(-19.6346030129934,-21.3499764596372,
8.87895960174956));
#153528=CARTESIAN_POINT('Ctrl Pts',(-19.716626443602,-21.3175402693169,
8.88334606376211));
#153529=CARTESIAN_POINT('Ctrl Pts',(-19.7966429339306,-21.2810319866776,
8.88773252577465));
#153530=CARTESIAN_POINT('Ctrl Pts',(-19.8766594242592,-21.2445237040383,
8.89211898778719));
#153531=CARTESIAN_POINT('Ctrl Pts',(-19.954668494674,-21.203943664325,8.89650544979973));
#153532=CARTESIAN_POINT('Ctrl Pts',(-20.0302483510423,-21.159564316712,
8.90089191181227));
#153533=CARTESIAN_POINT('Ctrl Pts',(-20.102350666183,-21.1172269286686,
8.90507654620531));
#153534=CARTESIAN_POINT('Ctrl Pts',(-20.1725107769709,-21.071274585504,
8.90926118059836));
#153535=CARTESIAN_POINT('Ctrl Pts',(-20.2403431519459,-21.0219107006307,
8.91344581499141));
#153536=CARTESIAN_POINT('Ctrl Pts',(-20.308078975931,-20.9726170791377,
8.91762449307535));
#153537=CARTESIAN_POINT('Ctrl Pts',(-20.3734932764658,-20.9199218296712,
8.92180317115929));
#153538=CARTESIAN_POINT('Ctrl Pts',(-20.4362266525525,-20.8640733310571,
8.92598184924322));
#153539=CARTESIAN_POINT('Ctrl Pts',(-20.50008447932,-20.807223788243,8.93023542712866));
#153540=CARTESIAN_POINT('Ctrl Pts',(-20.5611639093904,-20.7471070845338,
8.9344890050141));
#153541=CARTESIAN_POINT('Ctrl Pts',(-20.6191183231211,-20.6840302849064,
8.93874258289954));
#153542=CARTESIAN_POINT('Ctrl Pts',(-20.675949177453,-20.6221763521241,
8.94291369687749));
#153543=CARTESIAN_POINT('Ctrl Pts',(-20.7297747776525,-20.5574764280246,
8.94708481085544));
#153544=CARTESIAN_POINT('Ctrl Pts',(-20.7803043703346,-20.4902582435825,
8.95125592483339));
#153545=CARTESIAN_POINT('Ctrl Pts',(-20.8308170073239,-20.4230626148514,
8.95542563915376));
#153546=CARTESIAN_POINT('Ctrl Pts',(-20.8780355571481,-20.3533507714295,
8.95959535347413));
#153547=CARTESIAN_POINT('Ctrl Pts',(-20.9217100507378,-20.2814828821391,
8.9637650677945));
#153548=CARTESIAN_POINT('Ctrl Pts',(-20.9653829902015,-20.2096175502167,
8.96793463373855));
#153549=CARTESIAN_POINT('Ctrl Pts',(-21.005511885995,-20.1355967185424,
8.97210419968259));
#153550=CARTESIAN_POINT('Ctrl Pts',(-21.0418912815017,-20.0598076695746,
8.97627376562663));
#153551=CARTESIAN_POINT('Ctrl Pts',(-21.0795497316757,-19.9813539711409,
8.98058992836555));
#153552=CARTESIAN_POINT('Ctrl Pts',(-21.113189882732,-19.901005876374,8.98490609110447));
#153553=CARTESIAN_POINT('Ctrl Pts',(-21.1426376470827,-19.8192166309844,
8.9892222538434));
#153554=CARTESIAN_POINT('Ctrl Pts',(-21.171126153607,-19.7400916616608,
8.99339781803508));
#153555=CARTESIAN_POINT('Ctrl Pts',(-21.1956911205895,-19.6596184551168,
8.99757338222676));
#153556=CARTESIAN_POINT('Ctrl Pts',(-21.216225998462,-19.5782220792652,
9.00174894641843));
#153557=CARTESIAN_POINT('Ctrl Pts',(-21.2377980441989,-19.4927145659707,
9.00613540843098));
#153558=CARTESIAN_POINT('Ctrl Pts',(-21.254922068569,-19.4061887466987,
9.01052187044353));
#153559=CARTESIAN_POINT('Ctrl Pts',(-21.2675357890124,-19.3191463002581,
9.01490833245607));
#153560=CARTESIAN_POINT('Ctrl Pts',(-21.2801495094559,-19.2321038538175,
9.01929479446862));
#153561=CARTESIAN_POINT('Ctrl Pts',(-21.288252948244,-19.1445453649661,
9.02368125648116));
#153562=CARTESIAN_POINT('Ctrl Pts',(-21.2918468828523,-19.0569729673898,
9.02806771849371));
#153563=CARTESIAN_POINT('Ctrl Pts',(-21.2932731600888,-19.022219269613,
9.02980851558631));
#153564=CARTESIAN_POINT('Ctrl Pts',(-21.2939911726516,-18.9874363059255,
9.03154931267891));
#153565=CARTESIAN_POINT('Ctrl Pts',(-21.2939999191096,-18.9526435515772,
9.03329010977151));
#153566=CARTESIAN_POINT('',(-21.293999998394,-18.9519093211995,8.96670989026365));
#153567=CARTESIAN_POINT('Ctrl Pts',(-17.1744641402401,-20.9821349467765,
8.68337762424306));
#153568=CARTESIAN_POINT('Ctrl Pts',(-17.2410628670692,-21.0332956358081,
8.68754915470747));
#153569=CARTESIAN_POINT('Ctrl Pts',(-17.3102359477333,-21.0812173626802,
8.69172068517188));
#153570=CARTESIAN_POINT('Ctrl Pts',(-17.3816324675696,-21.1256379774995,
8.6958922156363));
#153571=CARTESIAN_POINT('Ctrl Pts',(-17.4530008754767,-21.170041101982,
8.70006210358691));
#153572=CARTESIAN_POINT('Ctrl Pts',(-17.5265905938739,-21.2109456092011,
8.70423199153752));
#153573=CARTESIAN_POINT('Ctrl Pts',(-17.6020217631817,-21.248132677214,
8.70840187948813));
#153574=CARTESIAN_POINT('Ctrl Pts',(-17.6774458595108,-21.2853162582951,
8.71257137643952));
#153575=CARTESIAN_POINT('Ctrl Pts',(-17.7547106507946,-21.3187828899485,
8.71674087339091));
#153576=CARTESIAN_POINT('Ctrl Pts',(-17.8334129450119,-21.3483603561209,
8.7209103703423));
#153577=CARTESIAN_POINT('Ctrl Pts',(-17.9121314679419,-21.3779439212794,
8.72508072705983));
#153578=CARTESIAN_POINT('Ctrl Pts',(-17.9922876513835,-21.4036365679451,
8.72925108377736));
#153579=CARTESIAN_POINT('Ctrl Pts',(-18.0734609565294,-21.4253152189017,
8.73342144049489));
#153580=CARTESIAN_POINT('Ctrl Pts',(-18.1547253310253,-21.4470181914091,
8.73759647598798));
#153581=CARTESIAN_POINT('Ctrl Pts',(-18.2370086591808,-21.4646980633853,
8.74177151148105));
#153582=CARTESIAN_POINT('Ctrl Pts',(-18.3198785149476,-21.4782825249006,
8.74594654697414));
#153583=CARTESIAN_POINT('Ctrl Pts',(-18.4028028717265,-21.4918759205077,
8.75012432826251));
#153584=CARTESIAN_POINT('Ctrl Pts',(-18.4863140672385,-21.5013684936004,
8.75430210955089));
#153585=CARTESIAN_POINT('Ctrl Pts',(-18.5699752029833,-21.506739882251,
8.75847989083926));
#153586=CARTESIAN_POINT('Ctrl Pts',(-18.6537709748597,-21.5121199150944,
8.76266439544433));
#153587=CARTESIAN_POINT('Ctrl Pts',(-18.7377167095927,-21.5133655229479,
8.76684890004941));
#153588=CARTESIAN_POINT('Ctrl Pts',(-18.8213766941403,-21.5105084157222,
8.77103340465448));
#153589=CARTESIAN_POINT('Ctrl Pts',(-18.8486819099696,-21.5095759038425,
8.77239915677598));
#153590=CARTESIAN_POINT('Ctrl Pts',(-18.8759567414457,-21.5082067564715,
8.77376490889747));
#153591=CARTESIAN_POINT('Ctrl Pts',(-18.9031862415111,-21.5064032601928,
8.77513066101897));
#153592=CARTESIAN_POINT('Ctrl Pts',(-18.9866168294529,-21.5008773873516,
8.77931529541202));
#153593=CARTESIAN_POINT('Ctrl Pts',(-19.0699316687706,-21.4912494832414,
8.78349992980506));
#153594=CARTESIAN_POINT('Ctrl Pts',(-19.1526949496533,-21.4775285662876,
8.78768456419811));
#153595=CARTESIAN_POINT('Ctrl Pts',(-19.2353404272495,-21.4638271793609,
8.79186324228203));
#153596=CARTESIAN_POINT('Ctrl Pts',(-19.3174354558603,-21.4460444262518,
8.79604192036597));
#153597=CARTESIAN_POINT('Ctrl Pts',(-19.3985474281615,-21.4242412333193,
8.8002205984499));
#153598=CARTESIAN_POINT('Ctrl Pts',(-19.4811132742725,-21.402047233823,
8.80447417633533));
#153599=CARTESIAN_POINT('Ctrl Pts',(-19.5626599937757,-21.3756872759161,
8.80872775422077));
#153600=CARTESIAN_POINT('Ctrl Pts',(-19.6427400986354,-21.3452804752331,
8.81298133210621));
#153601=CARTESIAN_POINT('Ctrl Pts',(-19.7212676943988,-21.3154631697154,
8.81715244608416));
#153602=CARTESIAN_POINT('Ctrl Pts',(-19.798384584547,-21.2817547038766,
8.82132356006211));
#153603=CARTESIAN_POINT('Ctrl Pts',(-19.8736839568159,-21.2443177089087,
8.82549467404006));
#153604=CARTESIAN_POINT('Ctrl Pts',(-19.9489580616533,-21.206893276286,
8.82966438836044));
#153605=CARTESIAN_POINT('Ctrl Pts',(-20.0224154482666,-21.1657430039572,
8.83383410268082));
#153606=CARTESIAN_POINT('Ctrl Pts',(-20.09367122156,-21.1210768011441,8.83800381700119));
#153607=CARTESIAN_POINT('Ctrl Pts',(-20.1649244592673,-21.0764121877461,
8.84217338294524));
#153608=CARTESIAN_POINT('Ctrl Pts',(-20.2339758500892,-21.0282321376739,
8.8463429488893));
#153609=CARTESIAN_POINT('Ctrl Pts',(-20.3004681352886,-20.9767907499605,
8.85051251483335));
#153610=CARTESIAN_POINT('Ctrl Pts',(-20.3692982072083,-20.9235407465149,
8.85482867757227));
#153611=CARTESIAN_POINT('Ctrl Pts',(-20.4353854517829,-20.8667961238597,
8.85914484031119));
#153612=CARTESIAN_POINT('Ctrl Pts',(-20.4983710832767,-20.8068840072891,
8.86346100305011));
#153613=CARTESIAN_POINT('Ctrl Pts',(-20.5593049644495,-20.7489235216142,
8.86763656724179));
#153614=CARTESIAN_POINT('Ctrl Pts',(-20.6173359087928,-20.6879991088312,
8.87181213143347));
#153615=CARTESIAN_POINT('Ctrl Pts',(-20.6721781340607,-20.6244429797901,
8.87598769562515));
#153616=CARTESIAN_POINT('Ctrl Pts',(-20.7297903097518,-20.5576767817615,
8.8803741576377));
#153617=CARTESIAN_POINT('Ctrl Pts',(-20.7838828183069,-20.4880064858705,
8.88476061965024));
#153618=CARTESIAN_POINT('Ctrl Pts',(-20.8341751072845,-20.4158526287652,
8.88914708166278));
#153619=CARTESIAN_POINT('Ctrl Pts',(-20.8844673962621,-20.3436987716599,
8.89353354367532));
#153620=CARTESIAN_POINT('Ctrl Pts',(-20.930959223453,-20.2690618860433,
8.89792000568786));
#153621=CARTESIAN_POINT('Ctrl Pts',(-20.9734262024012,-20.1923911818451,
8.9023064677004));
#153622=CARTESIAN_POINT('Ctrl Pts',(-21.0159038253685,-20.1157012607291,
8.90669402914565));
#153623=CARTESIAN_POINT('Ctrl Pts',(-21.0545007977188,-20.0367143701651,
8.9110815905909));
#153624=CARTESIAN_POINT('Ctrl Pts',(-21.0889748257324,-19.9558394145314,
8.91546915203614));
#153625=CARTESIAN_POINT('Ctrl Pts',(-21.1233545067051,-19.8751857940067,
8.91984470579146));
#153626=CARTESIAN_POINT('Ctrl Pts',(-21.1536335666925,-19.7926547636184,
8.92422025954678));
#153627=CARTESIAN_POINT('Ctrl Pts',(-21.1796158858339,-19.7086788876113,
8.92859581330209));
#153628=CARTESIAN_POINT('Ctrl Pts',(-21.2055560013419,-19.6248394154053,
8.9329642597524));
#153629=CARTESIAN_POINT('Ctrl Pts',(-21.227213143681,-19.5395601416149,
8.9373327062027));
#153630=CARTESIAN_POINT('Ctrl Pts',(-21.2444392039472,-19.4532933305808,
8.94170115265301));
#153631=CARTESIAN_POINT('Ctrl Pts',(-21.2616295048391,-19.3672055997974,
8.94606053069709));
#153632=CARTESIAN_POINT('Ctrl Pts',(-21.2744069696189,-19.2801348014838,
8.95041990874118));
#153633=CARTESIAN_POINT('Ctrl Pts',(-21.2826736357251,-19.1925466660746,
8.95477928678526));
#153634=CARTESIAN_POINT('Ctrl Pts',(-21.2902149496553,-19.1126438833585,
8.95875615459968));
#153635=CARTESIAN_POINT('Ctrl Pts',(-21.2940028463113,-19.0323109723971,
8.9627330224141));
#153636=CARTESIAN_POINT('Ctrl Pts',(-21.293999998394,-18.95190932191,8.96670989022851));
#153637=CARTESIAN_POINT('Ctrl Pts',(-21.293999998394,-18.9519093211995,
8.96670989026365));
#153638=CARTESIAN_POINT('Ctrl Pts',(-21.2939968622717,-18.8633718327361,
8.97108917708312));
#153639=CARTESIAN_POINT('Ctrl Pts',(-21.2893963356695,-18.7749281972304,
8.97546846390259));
#153640=CARTESIAN_POINT('Ctrl Pts',(-21.2802532223815,-18.6870575014991,
8.97984775072206));
#153641=CARTESIAN_POINT('Ctrl Pts',(-21.2710840473103,-18.5989363367038,
8.98423952038192));
#153642=CARTESIAN_POINT('Ctrl Pts',(-21.2573464424812,-18.5113917635122,
8.98863129004178));
#153643=CARTESIAN_POINT('Ctrl Pts',(-21.2391468026208,-18.4248951742595,
8.99302305970165));
#153644=CARTESIAN_POINT('Ctrl Pts',(-21.2209205771356,-18.3382722327336,
8.99742124475991));
#153645=CARTESIAN_POINT('Ctrl Pts',(-21.1982194166656,-18.2527007028949,
9.00181942981817));
#153646=CARTESIAN_POINT('Ctrl Pts',(-21.1711995861976,-18.1686366251616,
9.00621761487642));
#153647=CARTESIAN_POINT('Ctrl Pts',(-21.1441046030878,-18.0843387325816,
9.01062803299538));
#153648=CARTESIAN_POINT('Ctrl Pts',(-21.1126670698913,-18.0015570394273,
9.01503845111433));
#153649=CARTESIAN_POINT('Ctrl Pts',(-21.0770917883152,-17.9207285170577,
9.01944886923329));
#153650=CARTESIAN_POINT('Ctrl Pts',(-21.0501146625114,-17.859435362938,
9.02279333761614));
#153651=CARTESIAN_POINT('Ctrl Pts',(-21.0207591774504,-17.7992649146786,
9.02613780599899));
#153652=CARTESIAN_POINT('Ctrl Pts',(-20.9891316170539,-17.7403971815138,
9.02948227438184));
#153653=CARTESIAN_POINT('Ctrl Pts',(-20.949558877278,-17.6667412480012,
9.03366690877489));
#153654=CARTESIAN_POINT('Ctrl Pts',(-20.9063001320241,-17.5948890389388,
9.03785154316794));
#153655=CARTESIAN_POINT('Ctrl Pts',(-20.8595440286336,-17.5252335221418,
9.04203617756098));
#153656=CARTESIAN_POINT('Ctrl Pts',(-20.812854476769,-17.4556771513512,
9.04621485564493));
#153657=CARTESIAN_POINT('Ctrl Pts',(-20.7626777089518,-17.3883116408712,
9.05039353372888));
#153658=CARTESIAN_POINT('Ctrl Pts',(-20.7092482964897,-17.3235055519854,
9.05457221181283));
#153659=CARTESIAN_POINT('Ctrl Pts',(-20.6548612002084,-17.2575378605317,
9.05882578969826));
#153660=CARTESIAN_POINT('Ctrl Pts',(-20.5971039332157,-17.1942226731584,
9.06307936758369));
#153661=CARTESIAN_POINT('Ctrl Pts',(-20.5362701954422,-17.1339180044286,
9.06733294546913));
#153662=CARTESIAN_POINT('Ctrl Pts',(-20.4766158383827,-17.0747824593771,
9.07150405944708));
#153663=CARTESIAN_POINT('Ctrl Pts',(-20.4140035745828,-17.0185420838701,
9.07567517342503));
#153664=CARTESIAN_POINT('Ctrl Pts',(-20.3487498736144,-16.9654998500724,
9.07984628740299));
#153665=CARTESIAN_POINT('Ctrl Pts',(-20.2835180691556,-16.9124754151086,
9.08401600172336));
#153666=CARTESIAN_POINT('Ctrl Pts',(-20.2156469445306,-16.8626472804563,
9.08818571604373));
#153667=CARTESIAN_POINT('Ctrl Pts',(-20.1454869304126,-16.8162788933771,
9.0923554303641));
#153668=CARTESIAN_POINT('Ctrl Pts',(-20.0753294128889,-16.7699121562841,
9.09652499630815));
#153669=CARTESIAN_POINT('Ctrl Pts',(-20.0028835520724,-16.7270051749182,
9.10069456225219));
#153670=CARTESIAN_POINT('Ctrl Pts',(-19.9285285607302,-16.687777944282,
9.10486412819624));
#153671=CARTESIAN_POINT('Ctrl Pts',(-19.8515593396191,-16.6471715326087,
9.10918029093515));
#153672=CARTESIAN_POINT('Ctrl Pts',(-19.7725447065605,-16.6105086923156,
9.11349645367407));
#153673=CARTESIAN_POINT('Ctrl Pts',(-19.6919309796755,-16.577980573336,
9.11781261641299));
#153674=CARTESIAN_POINT('Ctrl Pts',(-19.6139432364648,-16.5465120544109,
9.12198818060467));
#153675=CARTESIAN_POINT('Ctrl Pts',(-19.5344594409716,-16.5189131263824,
9.12616374479635));
#153676=CARTESIAN_POINT('Ctrl Pts',(-19.4539003149004,-16.4953063812094,
9.13033930898803));
#153677=CARTESIAN_POINT('Ctrl Pts',(-19.3692723388825,-16.4705073154575,
9.13472577100056));
#153678=CARTESIAN_POINT('Ctrl Pts',(-19.2834581156085,-16.4501144565313,
9.1391122330131));
#153679=CARTESIAN_POINT('Ctrl Pts',(-19.1969566012278,-16.4342090663878,
9.14349869502564));
#153680=CARTESIAN_POINT('Ctrl Pts',(-19.1104550868471,-16.4183036762444,
9.14788515703818));
#153681=CARTESIAN_POINT('Ctrl Pts',(-19.0232668665414,-16.406885754803,
9.15227161905072));
#153682=CARTESIAN_POINT('Ctrl Pts',(-18.9358937423135,-16.3999735665917,
9.15665808106326));
#153683=CARTESIAN_POINT('Ctrl Pts',(-18.8525407850493,-16.3933794184063,
9.16084271545631));
#153684=CARTESIAN_POINT('Ctrl Pts',(-18.7687093097475,-16.3908609393394,
9.16502734984936));
#153685=CARTESIAN_POINT('Ctrl Pts',(-18.68483185138,-16.3924722128562,9.1692119842424));
#153686=CARTESIAN_POINT('Ctrl Pts',(-18.6010737821926,-16.3940811929246,
9.17339066232635));
#153687=CARTESIAN_POINT('Ctrl Pts',(-18.5172703159603,-16.3998082408783,
9.1775693404103));
#153688=CARTESIAN_POINT('Ctrl Pts',(-18.4338583233965,-16.4096556146018,
9.18174801849425));
#153689=CARTESIAN_POINT('Ctrl Pts',(-18.3489512308132,-16.4196794954222,
9.18600159637968));
#153690=CARTESIAN_POINT('Ctrl Pts',(-18.264450264908,-16.4339729066197,
9.19025517426512));
#153691=CARTESIAN_POINT('Ctrl Pts',(-18.1808154334733,-16.4524826795246,
9.19450875215055));
#153692=CARTESIAN_POINT('Ctrl Pts',(-18.0988020264459,-16.4706336043628,
9.1986798661285));
#153693=CARTESIAN_POINT('Ctrl Pts',(-18.0176219400175,-16.4928387610342,
9.20285098010646));
#153694=CARTESIAN_POINT('Ctrl Pts',(-17.9377012248092,-16.5189960417974,
9.20702209408441));
#153695=CARTESIAN_POINT('Ctrl Pts',(-17.8578073277689,-16.5451445452324,
9.21119180840478));
#153696=CARTESIAN_POINT('Ctrl Pts',(-17.7791723995178,-16.5752423959817,
9.21536152272515));
#153697=CARTESIAN_POINT('Ctrl Pts',(-17.7022076389884,-16.609137536312,
9.21953123704553));
#153698=CARTESIAN_POINT('Ctrl Pts',(-17.6252456171954,-16.6430314705078,
9.22370080298957));
#153699=CARTESIAN_POINT('Ctrl Pts',(-17.5499540656281,-16.6807222394303,
9.22787036893362));
#153700=CARTESIAN_POINT('Ctrl Pts',(-17.4767232259473,-16.7220100642766,
9.23203993487766));
#153701=CARTESIAN_POINT('Ctrl Pts',(-17.4009176802834,-16.7647495181104,
9.23635609761658));
#153702=CARTESIAN_POINT('Ctrl Pts',(-17.3273209113735,-16.811343420091,
9.2406722603555));
#153703=CARTESIAN_POINT('Ctrl Pts',(-17.2563352295956,-16.8615199531434,
9.24498842309442));
#153704=CARTESIAN_POINT('Ctrl Pts',(-17.1876618989352,-16.9100619909092,
9.2491639872861));
#153705=CARTESIAN_POINT('Ctrl Pts',(-17.1214324971171,-16.9619565080489,
9.25333955147778));
#153706=CARTESIAN_POINT('Ctrl Pts',(-17.0579778332574,-17.0169161008919,
9.25751511566946));
#153707=CARTESIAN_POINT('Ctrl Pts',(-16.9913182251753,-17.0746515721154,
9.261901577682));
#153708=CARTESIAN_POINT('Ctrl Pts',(-16.9277214465955,-17.135769485738,
9.26628803969454));
#153709=CARTESIAN_POINT('Ctrl Pts',(-16.8675259014641,-17.1998942841556,
9.27067450170708));
#153710=CARTESIAN_POINT('Ctrl Pts',(-16.8073303563327,-17.2640190825733,
9.27506096371962));
#153711=CARTESIAN_POINT('Ctrl Pts',(-16.7505363613297,-17.3311502736972,
9.27944742573217));
#153712=CARTESIAN_POINT('Ctrl Pts',(-16.6974308899392,-17.4008758076974,
9.28383388774471));
#153713=CARTESIAN_POINT('Ctrl Pts',(-16.6467688800086,-17.4673931665203,
9.28801852213775));
#153714=CARTESIAN_POINT('Ctrl Pts',(-16.5992748500801,-17.5365189656784,
9.2922031565308));
#153715=CARTESIAN_POINT('Ctrl Pts',(-16.5552283987657,-17.6079187860643,
9.29638779092385));
#153716=CARTESIAN_POINT('Ctrl Pts',(-16.5112446421229,-17.6792169776433,
9.3005664690078));
#153717=CARTESIAN_POINT('Ctrl Pts',(-16.4706989563139,-17.7527823729939,
9.30474514709174));
#153718=CARTESIAN_POINT('Ctrl Pts',(-16.4338297096935,-17.8282488551323,
9.30892382517568));
#153719=CARTESIAN_POINT('Ctrl Pts',(-16.3962996083249,-17.9050680197263,
9.31317740306112));
#153720=CARTESIAN_POINT('Ctrl Pts',(-16.3625793350038,-17.9838567118701,
9.31743098094656));
#153721=CARTESIAN_POINT('Ctrl Pts',(-16.3328731767861,-18.0641993586154,
9.32168455883199));
#153722=CARTESIAN_POINT('Ctrl Pts',(-16.3037429304123,-18.1429844063778,
9.32585567280995));
#153723=CARTESIAN_POINT('Ctrl Pts',(-16.2784727120491,-18.223263242189,
9.33002678678789));
#153724=CARTESIAN_POINT('Ctrl Pts',(-16.2572072783656,-18.3046223559168,
9.33419790076585));
#153725=CARTESIAN_POINT('Ctrl Pts',(-16.2359489805037,-18.3859541688082,
9.33836761508622));
#153726=CARTESIAN_POINT('Ctrl Pts',(-16.2186929146628,-18.4683650949799,
9.34253732940659));
#153727=CARTESIAN_POINT('Ctrl Pts',(-16.2055337985359,-18.5514270752364,
9.34670704372697));
#153728=CARTESIAN_POINT('Ctrl Pts',(-16.1923751506668,-18.6344860997912,
9.35087660967101));
#153729=CARTESIAN_POINT('Ctrl Pts',(-16.183313233791,-18.7181956778687,
9.35504617561505));
#153730=CARTESIAN_POINT('Ctrl Pts',(-16.1783912959603,-18.8021195415123,
9.3592157415591));
#153731=CARTESIAN_POINT('Ctrl Pts',(-16.1732963088673,-18.8889940646704,
9.36353190429802));
#153732=CARTESIAN_POINT('Ctrl Pts',(-16.1726378716504,-18.9760976958013,
9.36784806703694));
#153733=CARTESIAN_POINT('Ctrl Pts',(-16.1764051921424,-19.0629450261169,
9.37216422977586));
#153734=CARTESIAN_POINT('Ctrl Pts',(-16.1800497925657,-19.1469633137821,
9.37633979396754));
#153735=CARTESIAN_POINT('Ctrl Pts',(-16.1878361499306,-19.2307412775514,
9.38051535815922));
#153736=CARTESIAN_POINT('Ctrl Pts',(-16.1997016639331,-19.3138451931539,
9.3846909223509));
#153737=CARTESIAN_POINT('Ctrl Pts',(-16.2121664768403,-19.4011464899727,
9.38907738436344));
#153738=CARTESIAN_POINT('Ctrl Pts',(-16.2291332400404,-19.487703283801,
9.39346384637598));
#153739=CARTESIAN_POINT('Ctrl Pts',(-16.2504693406595,-19.5730277482654,
9.39785030838853));
#153740=CARTESIAN_POINT('Ctrl Pts',(-16.2718054412786,-19.6583522127299,
9.40223677040107));
#153741=CARTESIAN_POINT('Ctrl Pts',(-16.2975106369606,-19.7424438151944,
9.4066232324136));
#153742=CARTESIAN_POINT('Ctrl Pts',(-16.3273937923111,-19.8248382216157,
9.41100969442614));
#153743=CARTESIAN_POINT('Ctrl Pts',(-16.3558995253323,-19.9034347728948,
9.41519396859567));
#153744=CARTESIAN_POINT('Ctrl Pts',(-16.3883126378462,-19.9807796693235,
9.4193782427652));
#153745=CARTESIAN_POINT('Ctrl Pts',(-16.4245033134343,-20.0564569048823,
9.42356251693473));
#153746=CARTESIAN_POINT('Ctrl Pts',(-16.4606449440058,-20.1320315838787,
9.42774112064377));
#153747=CARTESIAN_POINT('Ctrl Pts',(-16.5005537757621,-20.2059426782427,
9.4319197243528));
#153748=CARTESIAN_POINT('Ctrl Pts',(-16.5440510006887,-20.2777916051988,
9.43609832806183));
#153749=CARTESIAN_POINT('Ctrl Pts',(-16.5874980215242,-20.3495576047938,
9.44027210886545));
#153750=CARTESIAN_POINT('Ctrl Pts',(-16.6345249665291,-20.4192657763403,
9.44444588966907));
#153751=CARTESIAN_POINT('Ctrl Pts',(-16.6849066106161,-20.48654106546,9.44861967047269));
#153752=CARTESIAN_POINT('Ctrl Pts',(-16.7352537173085,-20.5537702363309,
9.45279059008516));
#153753=CARTESIAN_POINT('Ctrl Pts',(-16.7889506803368,-20.6185694703229,
9.45696150969763));
#153754=CARTESIAN_POINT('Ctrl Pts',(-16.8457290001202,-20.6805926735391,
9.4611324293101));
#153755=CARTESIAN_POINT('Ctrl Pts',(-16.9024956626461,-20.7426031426614,
9.46530249258366));
#153756=CARTESIAN_POINT('Ctrl Pts',(-16.9623421216309,-20.8018383679809,
9.46947255585723));
#153757=CARTESIAN_POINT('Ctrl Pts',(-17.0249603575963,-20.8579862278339,
9.47364261913079));
#153758=CARTESIAN_POINT('Ctrl Pts',(-17.0732023522128,-20.9012433511144,
9.47685529618713));
#153759=CARTESIAN_POINT('Ctrl Pts',(-17.1230886546779,-20.9426686481572,
9.48006797324345));
#153760=CARTESIAN_POINT('Ctrl Pts',(-17.1744641402402,-20.9821349467765,
9.48328065029978));
#153761=CARTESIAN_POINT('Origin',(-18.734,-18.952,-1.76670989022851));
#153762=CARTESIAN_POINT('',(-17.1744641402401,-20.9821349467765,10.3499274704374));
#153763=CARTESIAN_POINT('',(-17.1744641402401,-20.9821349467765,10.2832382127855));
#153764=CARTESIAN_POINT('',(-17.1744641402401,-20.9821349467765,-1.76670989022851));
#153765=CARTESIAN_POINT('',(-21.2939992159918,-18.9540035272626,9.8332901097715));
#153766=CARTESIAN_POINT('Ctrl Pts',(-21.2939992159918,-18.9540035272626,
9.8332901097715));
#153767=CARTESIAN_POINT('Ctrl Pts',(-21.2940649620946,-18.8699966984849,
9.83745593779552));
#153768=CARTESIAN_POINT('Ctrl Pts',(-21.2899913508454,-18.7859395799201,
9.84162176581954));
#153769=CARTESIAN_POINT('Ctrl Pts',(-21.281790209728,-18.7022700514273,
9.84578759384357));
#153770=CARTESIAN_POINT('Ctrl Pts',(-21.2735905258927,-18.6186153903907,
9.84995268163077));
#153771=CARTESIAN_POINT('Ctrl Pts',(-21.2612648140692,-18.5353486407622,
9.85411776941798));
#153772=CARTESIAN_POINT('Ctrl Pts',(-21.244876840873,-18.4529033260305,
9.85828285720518));
#153773=CARTESIAN_POINT('Ctrl Pts',(-21.2284868533626,-18.3704478776001,
9.86244845694076));
#153774=CARTESIAN_POINT('Ctrl Pts',(-21.2080337038202,-18.2888145159798,
9.86661405667634));
#153775=CARTESIAN_POINT('Ctrl Pts',(-21.183632148948,-18.2084259721853,
9.87077965641192));
#153776=CARTESIAN_POINT('Ctrl Pts',(-21.1592030081949,-18.1279465493957,
9.87494996534485));
#153777=CARTESIAN_POINT('Ctrl Pts',(-21.1308166833998,-18.0487151959126,
9.87912027427778));
#153778=CARTESIAN_POINT('Ctrl Pts',(-21.0986375209737,-17.9711384427947,
9.88329058321071));
#153779=CARTESIAN_POINT('Ctrl Pts',(-21.0664396371008,-17.8935165564616,
9.88746331837886));
#153780=CARTESIAN_POINT('Ctrl Pts',(-21.0304447198543,-17.8175516031279,
9.89163605354701));
#153781=CARTESIAN_POINT('Ctrl Pts',(-20.9908638255707,-17.7436268486802,
9.89580878871516));
#153782=CARTESIAN_POINT('Ctrl Pts',(-20.951210438291,-17.6695666999462,
9.89998916630977));
#153783=CARTESIAN_POINT('Ctrl Pts',(-20.9079581930336,-17.5975546086432,
9.90416954390439));
#153784=CARTESIAN_POINT('Ctrl Pts',(-20.8613622504217,-17.5279459787351,
9.90834992149901));
#153785=CARTESIAN_POINT('Ctrl Pts',(-20.8243993123259,-17.4727278774585,
9.91166606942059));
#153786=CARTESIAN_POINT('Ctrl Pts',(-20.7853331875372,-17.4190216712153,
9.91498221734217));
#153787=CARTESIAN_POINT('Ctrl Pts',(-20.7443085775785,-17.3669891410737,
9.91829836526374));
#153788=CARTESIAN_POINT('Ctrl Pts',(-20.6925397790042,-17.3013294900759,
9.92248299965679));
#153789=CARTESIAN_POINT('Ctrl Pts',(-20.6374544461771,-17.2380865845811,
9.92666763404984));
#153790=CARTESIAN_POINT('Ctrl Pts',(-20.5793066365797,-17.1776146368404,
9.93085226844289));
#153791=CARTESIAN_POINT('Ctrl Pts',(-20.521241593192,-17.1172287634325,
9.93503094652683));
#153792=CARTESIAN_POINT('Ctrl Pts',(-20.4601230476225,-17.0596063422905,
9.93920962461077));
#153793=CARTESIAN_POINT('Ctrl Pts',(-20.3962460420502,-17.0050695709172,
9.94338830269472));
#153794=CARTESIAN_POINT('Ctrl Pts',(-20.3312240870606,-16.949555267112,
9.94764188058015));
#153795=CARTESIAN_POINT('Ctrl Pts',(-20.263344107106,-16.8972387002909,
9.95189545846559));
#153796=CARTESIAN_POINT('Ctrl Pts',(-20.1929575410584,-16.8484214078412,
9.95614903635103));
#153797=CARTESIAN_POINT('Ctrl Pts',(-20.1239355559416,-16.8005505338647,
9.96032015032898));
#153798=CARTESIAN_POINT('Ctrl Pts',(-20.0525037029719,-16.7560447387741,
9.96449126430694));
#153799=CARTESIAN_POINT('Ctrl Pts',(-19.9790262804937,-16.7151473984905,
9.96866237828489));
#153800=CARTESIAN_POINT('Ctrl Pts',(-19.9055735140743,-16.6742637817043,
9.97283209260526));
#153801=CARTESIAN_POINT('Ctrl Pts',(-19.8300769429974,-16.6369864384996,
9.97700180692563));
#153802=CARTESIAN_POINT('Ctrl Pts',(-19.7529274425305,-16.6035139202332,
9.981171521246));
#153803=CARTESIAN_POINT('Ctrl Pts',(-19.675780687374,-16.5700425930628,
9.98534108719005));
#153804=CARTESIAN_POINT('Ctrl Pts',(-19.5969815421364,-16.5403760039565,
9.9895106531341));
#153805=CARTESIAN_POINT('Ctrl Pts',(-19.5169416763858,-16.5146649119626,
9.99368021907814));
#153806=CARTESIAN_POINT('Ctrl Pts',(-19.4340877076953,-16.4880498496923,
9.99799638181706));
#153807=CARTESIAN_POINT('Ctrl Pts',(-19.3499046498554,-16.4656737716516,
10.002312544556));
#153808=CARTESIAN_POINT('Ctrl Pts',(-19.2648652451189,-16.4476473707713,
10.0066287072949));
#153809=CARTESIAN_POINT('Ctrl Pts',(-19.1825959900471,-16.4302081780036,
10.0108042714866));
#153810=CARTESIAN_POINT('Ctrl Pts',(-19.0995257948676,-16.4168396609884,
10.0149798356783));
#153811=CARTESIAN_POINT('Ctrl Pts',(-19.0160902825551,-16.4075894449818,
10.01915539987));
#153812=CARTESIAN_POINT('Ctrl Pts',(-18.9284406408648,-16.397872022555,
10.0235418618825));
#153813=CARTESIAN_POINT('Ctrl Pts',(-18.8403883907188,-16.3926998996315,
10.027928323895));
#153814=CARTESIAN_POINT('Ctrl Pts',(-18.7524390182801,-16.3920664066025,
10.0323147859076));
#153815=CARTESIAN_POINT('Ctrl Pts',(-18.6644896458415,-16.3914329135735,
10.0367012479201));
#153816=CARTESIAN_POINT('Ctrl Pts',(-18.5766437273767,-16.395337948682,
10.0410877099327));
#153817=CARTESIAN_POINT('Ctrl Pts',(-18.4893986055749,-16.403712308658,
10.0454741719452));
#153818=CARTESIAN_POINT('Ctrl Pts',(-18.4061677611554,-16.4117013519176,
10.0496588063382));
#153819=CARTESIAN_POINT('Ctrl Pts',(-18.3231738401578,-16.4237872141345,
10.0538434407313));
#153820=CARTESIAN_POINT('Ctrl Pts',(-18.2408521955264,-16.4399480015448,
10.0580280751243));
#153821=CARTESIAN_POINT('Ctrl Pts',(-18.1586477255668,-16.4560857860745,
10.0622067532083));
#153822=CARTESIAN_POINT('Ctrl Pts',(-18.0771140788203,-16.4762868870104,
10.0663854312922));
#153823=CARTESIAN_POINT('Ctrl Pts',(-17.9966818731335,-16.5004776199688,
10.0705641093762));
#153824=CARTESIAN_POINT('Ctrl Pts',(-17.9148079779654,-16.5251019544298,
10.0748176872616));
#153825=CARTESIAN_POINT('Ctrl Pts',(-17.8340758788413,-16.5538603099738,
10.079071265147));
#153826=CARTESIAN_POINT('Ctrl Pts',(-17.7549293481803,-16.5866203985945,
10.0833248430325));
#153827=CARTESIAN_POINT('Ctrl Pts',(-17.677317227458,-16.6187453689711,
10.0874959570104));
#153828=CARTESIAN_POINT('Ctrl Pts',(-17.6012301897814,-16.6547181102195,
10.0916670709884));
#153829=CARTESIAN_POINT('Ctrl Pts',(-17.5270700635694,-16.6943640398533,
10.0958381849663));
#153830=CARTESIAN_POINT('Ctrl Pts',(-17.452934822504,-16.7339966659125,
10.1000078992867));
#153831=CARTESIAN_POINT('Ctrl Pts',(-17.380725614118,-16.7772998157408,
10.1041776136071));
#153832=CARTESIAN_POINT('Ctrl Pts',(-17.3108209620502,-16.8240522971792,
10.1083473279274));
#153833=CARTESIAN_POINT('Ctrl Pts',(-17.24091879749,-16.8708031149637,10.1125168938715));
#153834=CARTESIAN_POINT('Ctrl Pts',(-17.1733214081181,-16.9210027638615,
10.1166864598155));
#153835=CARTESIAN_POINT('Ctrl Pts',(-17.1083783873652,-16.9743866979274,
10.1208560257596));
#153836=CARTESIAN_POINT('Ctrl Pts',(-17.0411520501183,-17.029647545259,
10.1251721884985));
#153837=CARTESIAN_POINT('Ctrl Pts',(-16.9767706170265,-17.088320427997,
10.1294883512374));
#153838=CARTESIAN_POINT('Ctrl Pts',(-16.9155830497419,-17.1500677607041,
10.1338045139763));
#153839=CARTESIAN_POINT('Ctrl Pts',(-16.8563886610259,-17.2098036805428,
10.137980078168));
#153840=CARTESIAN_POINT('Ctrl Pts',(-16.8001835327301,-17.2724164438389,
10.1421556423597));
#153841=CARTESIAN_POINT('Ctrl Pts',(-16.7472435046119,-17.3375655392575,
10.1463312065513));
#153842=CARTESIAN_POINT('Ctrl Pts',(-16.6916296015263,-17.4060051606084,
10.1507176685639));
#153843=CARTESIAN_POINT('Ctrl Pts',(-16.6396196516928,-17.4772435963691,
10.1551041305764));
#153844=CARTESIAN_POINT('Ctrl Pts',(-16.5914816570985,-17.5508522025387,
10.159490592589));
#153845=CARTESIAN_POINT('Ctrl Pts',(-16.5433436625043,-17.6244608087082,
10.1638770546015));
#153846=CARTESIAN_POINT('Ctrl Pts',(-16.49907784951,-17.7004390456585,10.1682635166141));
#153847=CARTESIAN_POINT('Ctrl Pts',(-16.4588952312818,-17.7783312684767,
10.1726499786266));
#153848=CARTESIAN_POINT('Ctrl Pts',(-16.4205614748832,-17.8526395546591,
10.1768346130196));
#153849=CARTESIAN_POINT('Ctrl Pts',(-16.3858007370466,-17.9289661561368,
10.1810192474127));
#153850=CARTESIAN_POINT('Ctrl Pts',(-16.3548302568731,-18.0069331593007,
10.1852038818057));
#153851=CARTESIAN_POINT('Ctrl Pts',(-16.3239038593448,-18.0847891860859,
10.1893825598897));
#153852=CARTESIAN_POINT('Ctrl Pts',(-16.2967571717624,-18.1642805528127,
10.1935612379736));
#153853=CARTESIAN_POINT('Ctrl Pts',(-16.2735613224931,-18.2450052940595,
10.1977399160576));
#153854=CARTESIAN_POINT('Ctrl Pts',(-16.2499497042961,-18.3271769682774,
10.201993493943));
#153855=CARTESIAN_POINT('Ctrl Pts',(-16.2304321761497,-18.4106262399197,
10.2062470718284));
#153856=CARTESIAN_POINT('Ctrl Pts',(-16.2151377103691,-18.4949083616217,
10.2105006497139));
#153857=CARTESIAN_POINT('Ctrl Pts',(-16.2001397576524,-18.5775565099315,
10.2146717636918));
#153858=CARTESIAN_POINT('Ctrl Pts',(-16.1892026698429,-18.6610050301436,
10.2188428776698));
#153859=CARTESIAN_POINT('Ctrl Pts',(-16.1823971528,-18.7448215499598,10.2230139916477));
#153860=CARTESIAN_POINT('Ctrl Pts',(-16.1755939194141,-18.8286099443332,
10.2271837059681));
#153861=CARTESIAN_POINT('Ctrl Pts',(-16.1729195406043,-18.9127656349237,
10.2313534202885));
#153862=CARTESIAN_POINT('Ctrl Pts',(-16.1743929164357,-18.9968506161333,
10.2355231346088));
#153863=CARTESIAN_POINT('Ctrl Pts',(-16.1758662398381,-19.0809326052385,
10.2396927005529));
#153864=CARTESIAN_POINT('Ctrl Pts',(-16.1814870155134,-19.1649434300184,
10.2438622664969));
#153865=CARTESIAN_POINT('Ctrl Pts',(-16.1912220304804,-19.2484459440194,
10.248031832441));
#153866=CARTESIAN_POINT('Ctrl Pts',(-16.2012993165641,-19.3348843034011,
10.2523479951799));
#153867=CARTESIAN_POINT('Ctrl Pts',(-16.2157854771197,-19.4207774186556,
10.2566641579188));
#153868=CARTESIAN_POINT('Ctrl Pts',(-16.2345855425419,-19.505649139663,
10.2609803206577));
#153869=CARTESIAN_POINT('Ctrl Pts',(-16.2527731978104,-19.5877561732855,
10.2651558848494));
#153870=CARTESIAN_POINT('Ctrl Pts',(-16.274997853126,-19.6689068927551,
10.2693314490411));
#153871=CARTESIAN_POINT('Ctrl Pts',(-16.3011224991718,-19.7486850481613,
10.2735070132328));
#153872=CARTESIAN_POINT('Ctrl Pts',(-16.3285666389839,-19.8324926085424,
10.2778934752453));
#153873=CARTESIAN_POINT('Ctrl Pts',(-16.3603148903336,-19.9147847597328,
10.2822799372579));
#153874=CARTESIAN_POINT('Ctrl Pts',(-16.3961518958431,-19.9951041376056,
10.2866663992704));
#153875=CARTESIAN_POINT('Ctrl Pts',(-16.4319889013526,-20.0754235154785,
10.2910528612829));
#153876=CARTESIAN_POINT('Ctrl Pts',(-16.4719143298048,-20.1537696376098,
10.2954393232955));
#153877=CARTESIAN_POINT('Ctrl Pts',(-16.5156592733601,-20.2297184433711,
10.299825785308));
#153878=CARTESIAN_POINT('Ctrl Pts',(-16.5573791055785,-20.3021513047724,
10.3040091821608));
#153879=CARTESIAN_POINT('Ctrl Pts',(-16.6027278790407,-20.3726734305059,
10.3081925790136));
#153880=CARTESIAN_POINT('Ctrl Pts',(-16.6515056001626,-20.4408979396339,
10.3123759758664));
#153881=CARTESIAN_POINT('Ctrl Pts',(-16.7002227477719,-20.5090377256943,
10.3165541776622));
#153882=CARTESIAN_POINT('Ctrl Pts',(-16.7523601281892,-20.5748851865602,
10.320732379458));
#153883=CARTESIAN_POINT('Ctrl Pts',(-16.8076724802166,-20.6380789680573,
10.3249105812538));
#153884=CARTESIAN_POINT('Ctrl Pts',(-16.8629267562013,-20.7012063982853,
10.3290843960833));
#153885=CARTESIAN_POINT('Ctrl Pts',(-16.9213490806984,-20.761685339555,
10.3332582109128));
#153886=CARTESIAN_POINT('Ctrl Pts',(-16.9826524926142,-20.8191855580991,
10.3374320257423));
#153887=CARTESIAN_POINT('Ctrl Pts',(-17.0438286128232,-20.8765663819678,
10.341597173974));
#153888=CARTESIAN_POINT('Ctrl Pts',(-17.1078735520966,-20.9309805098277,
10.3457623222057));
#153889=CARTESIAN_POINT('Ctrl Pts',(-17.1744641402401,-20.9821349467765,
10.3499274704374));
#153890=CARTESIAN_POINT('Ctrl Pts',(-17.1725833834245,-20.9846205132764,
9.54996331522893));
#153891=CARTESIAN_POINT('Ctrl Pts',(-17.7798204361626,-21.4438297111124,
9.58795779411958));
#153892=CARTESIAN_POINT('Ctrl Pts',(-19.5298543219429,-21.8241544890203,
9.66834420857071));
#153893=CARTESIAN_POINT('Ctrl Pts',(-21.1196059552395,-20.3720005573578,
9.76278617060466));
#153894=CARTESIAN_POINT('Ctrl Pts',(-21.2937096219977,-19.2372014343179,
9.81923365374796));
#153895=CARTESIAN_POINT('Ctrl Pts',(-21.2916488755515,-18.9540199903513,
9.83328920133079));
#153896=CARTESIAN_POINT('',(-21.2939989766127,-18.9497109517324,9.7667098901893));
#153897=CARTESIAN_POINT('Ctrl Pts',(-17.1744641402402,-20.9821349467765,
9.48328065029978));
#153898=CARTESIAN_POINT('Ctrl Pts',(-17.2411530785286,-21.0333649356377,
9.48745092761406));
#153899=CARTESIAN_POINT('Ctrl Pts',(-17.3103520349426,-21.0812924251398,
9.49162120492833));
#153900=CARTESIAN_POINT('Ctrl Pts',(-17.3816948054842,-21.125676760902,
9.49579148224261));
#153901=CARTESIAN_POINT('Ctrl Pts',(-17.4531169624092,-21.170110485157,
9.49996640001634));
#153902=CARTESIAN_POINT('Ctrl Pts',(-17.5266873027709,-21.2109929445286,
9.50414131779007));
#153903=CARTESIAN_POINT('Ctrl Pts',(-17.6020133887381,-21.2481285486496,
9.5083162355638));
#153904=CARTESIAN_POINT('Ctrl Pts',(-17.6773879055774,-21.2852880290901,
9.51249383759898));
#153905=CARTESIAN_POINT('Ctrl Pts',(-17.7545199929606,-21.3186956771203,
9.51667143963415));
#153906=CARTESIAN_POINT('Ctrl Pts',(-17.8329977297368,-21.3482042711298,
9.52084904166933));
#153907=CARTESIAN_POINT('Ctrl Pts',(-17.9116029975094,-21.377760818362,
9.52503343255664));
#153908=CARTESIAN_POINT('Ctrl Pts',(-17.9915578414719,-21.4034055266289,
9.52921782344394));
#153909=CARTESIAN_POINT('Ctrl Pts',(-18.0724361918796,-21.4250413113786,
9.53340221433124));
#153910=CARTESIAN_POINT('Ctrl Pts',(-18.1032542451651,-21.4332854553792,
9.53499664325669));
#153911=CARTESIAN_POINT('Ctrl Pts',(-18.1342062953107,-21.4409480643631,
9.53659107218214));
#153912=CARTESIAN_POINT('Ctrl Pts',(-18.1652685194105,-21.4480257416514,
9.53818550110758));
#153913=CARTESIAN_POINT('Ctrl Pts',(-18.2467924112678,-21.4666013528503,
9.54237013550063));
#153914=CARTESIAN_POINT('Ctrl Pts',(-18.3293790330749,-21.4812132961356,
9.54655476989367));
#153915=CARTESIAN_POINT('Ctrl Pts',(-18.4126082132397,-21.4917455225678,
9.55073940428672));
#153916=CARTESIAN_POINT('Ctrl Pts',(-18.4957189269683,-21.5022627576792,
9.55491808237066));
#153917=CARTESIAN_POINT('Ctrl Pts',(-18.5794699298769,-21.508711753151,
9.55909676045461));
#153918=CARTESIAN_POINT('Ctrl Pts',(-18.663429267508,-21.5110271142986,
9.56327543853855));
#153919=CARTESIAN_POINT('Ctrl Pts',(-18.7488935159257,-21.5133839766308,
9.56752901642398));
#153920=CARTESIAN_POINT('Ctrl Pts',(-18.8345731712378,-21.5114574491382,
9.57178259430942));
#153921=CARTESIAN_POINT('Ctrl Pts',(-18.9200053717026,-21.5052336363321,
9.57603617219486));
#153922=CARTESIAN_POINT('Ctrl Pts',(-19.0037813022541,-21.499130484282,
9.58020728617281));
#153923=CARTESIAN_POINT('Ctrl Pts',(-19.0873188071793,-21.4888952174951,
9.58437840015076));
#153924=CARTESIAN_POINT('Ctrl Pts',(-19.1701815497897,-21.4745672747467,
9.58854951412871));
#153925=CARTESIAN_POINT('Ctrl Pts',(-19.2530164870065,-21.4602441398779,
9.59271922844908));
#153926=CARTESIAN_POINT('Ctrl Pts',(-19.3351766586592,-21.4418311348332,
9.59688894276945));
#153927=CARTESIAN_POINT('Ctrl Pts',(-19.4162332022014,-21.4194192707795,
9.60105865708982));
#153928=CARTESIAN_POINT('Ctrl Pts',(-19.497286861404,-21.3970082042361,
9.60522822303387));
#153929=CARTESIAN_POINT('Ctrl Pts',(-19.5772365274095,-21.3705986850247,
9.60939778897791));
#153930=CARTESIAN_POINT('Ctrl Pts',(-19.6556671754965,-21.3403319739124,
9.61356735492196));
#153931=CARTESIAN_POINT('Ctrl Pts',(-19.7368553484155,-21.3090011225755,
9.61788351766088));
#153932=CARTESIAN_POINT('Ctrl Pts',(-19.8164152065819,-21.2735369848544,
9.6221996803998));
#153933=CARTESIAN_POINT('Ctrl Pts',(-19.8939093684295,-21.2341503581117,
9.62651584313872));
#153934=CARTESIAN_POINT('Ctrl Pts',(-19.9688791661059,-21.1960467465925,
9.63069140733039));
#153935=CARTESIAN_POINT('Ctrl Pts',(-20.0419153954164,-21.1542725466308,
9.63486697152208));
#153936=CARTESIAN_POINT('Ctrl Pts',(-20.112649171425,-21.1090643157146,
9.63904253571376));
#153937=CARTESIAN_POINT('Ctrl Pts',(-20.1869555423062,-21.0615727245271,
9.6434289977263));
#153938=CARTESIAN_POINT('Ctrl Pts',(-20.2587202783153,-21.0102914191921,
9.64781545973884));
#153939=CARTESIAN_POINT('Ctrl Pts',(-20.3275542346358,-20.9555430869523,
9.65220192175138));
#153940=CARTESIAN_POINT('Ctrl Pts',(-20.3963881909563,-20.9007947547124,
9.65658838376392));
#153941=CARTESIAN_POINT('Ctrl Pts',(-20.4622909830917,-20.8425798367028,
9.66097484577646));
#153942=CARTESIAN_POINT('Ctrl Pts',(-20.5249190804939,-20.7812645645513,
9.665361307789));
#153943=CARTESIAN_POINT('Ctrl Pts',(-20.5852113014986,-20.722236203594,
9.66958416538901));
#153944=CARTESIAN_POINT('Ctrl Pts',(-20.6427127908697,-20.6600954577448,
9.67380702298902));
#153945=CARTESIAN_POINT('Ctrl Pts',(-20.6970796830689,-20.5951427685755,
9.67802988058904));
#153946=CARTESIAN_POINT('Ctrl Pts',(-20.7500936846377,-20.5318063918539,
9.68214765466763));
#153947=CARTESIAN_POINT('Ctrl Pts',(-20.8001269202378,-20.465796754398,
9.68626542874623));
#153948=CARTESIAN_POINT('Ctrl Pts',(-20.8468954124061,-20.3974317611819,
9.69038320282483));
#153949=CARTESIAN_POINT('Ctrl Pts',(-20.89361966769,-20.3291314323191,9.69449708202704));
#153950=CARTESIAN_POINT('Ctrl Pts',(-20.9370850392269,-20.2584805564847,
9.69861096122924));
#153951=CARTESIAN_POINT('Ctrl Pts',(-20.9770478427321,-20.1858299620349,
9.70272484043145));
#153952=CARTESIAN_POINT('Ctrl Pts',(-21.0169856434319,-20.1132248215702,
9.70683614577717));
#153953=CARTESIAN_POINT('Ctrl Pts',(-21.0534249974543,-20.038622860247,
9.71094745112288));
#153954=CARTESIAN_POINT('Ctrl Pts',(-21.0861664418207,-19.9624024099201,
9.7150587564686));
#153955=CARTESIAN_POINT('Ctrl Pts',(-21.1204445396302,-19.88260470698,9.71936301761199));
#153956=CARTESIAN_POINT('Ctrl Pts',(-21.1506688210158,-19.8010333411259,
9.72366727875538));
#153957=CARTESIAN_POINT('Ctrl Pts',(-21.1766659614561,-19.7181481584811,
9.72797153989877));
#153958=CARTESIAN_POINT('Ctrl Pts',(-21.2014998963995,-19.6389715567968,
9.73208321292912));
#153959=CARTESIAN_POINT('Ctrl Pts',(-21.222476755318,-19.5585966865054,
9.73619488595946));
#153960=CARTESIAN_POINT('Ctrl Pts',(-21.2394965458156,-19.4774398718274,
9.74030655898981));
#153961=CARTESIAN_POINT('Ctrl Pts',(-21.2565208804896,-19.3962613887936,
9.74441932981082));
#153962=CARTESIAN_POINT('Ctrl Pts',(-21.2695859645564,-19.3143010135805,
9.74853210063183));
#153963=CARTESIAN_POINT('Ctrl Pts',(-21.2786432445868,-19.2319834955467,
9.75264487145285));
#153964=CARTESIAN_POINT('Ctrl Pts',(-21.2877094512626,-19.1495848472747,
9.75676169572548));
#153965=CARTESIAN_POINT('Ctrl Pts',(-21.2927599450141,-19.066828826857,
9.76087851999811));
#153966=CARTESIAN_POINT('Ctrl Pts',(-21.2937982075177,-18.9841424452888,
9.76499534427074));
#153967=CARTESIAN_POINT('Ctrl Pts',(-21.2939423435977,-18.9726635650768,
9.76556685957692));
#153968=CARTESIAN_POINT('Ctrl Pts',(-21.2940092371596,-18.9611860219109,
9.76613837488311));
#153969=CARTESIAN_POINT('Ctrl Pts',(-21.2939989766127,-18.9497109517324,
9.7667098901893));
#153970=CARTESIAN_POINT('Ctrl Pts',(-21.293998976612,-18.9497109509451,
9.76670989022851));
#153971=CARTESIAN_POINT('Ctrl Pts',(-21.2938920610985,-18.8301400729742,
9.77266511192846));
#153972=CARTESIAN_POINT('Ctrl Pts',(-21.2854044483395,-18.7109297707717,
9.77862033362841));
#153973=CARTESIAN_POINT('Ctrl Pts',(-21.2687069780221,-18.5930285031284,
9.78457555532836));
#153974=CARTESIAN_POINT('Ctrl Pts',(-21.2612660069352,-18.5404876147807,
9.78722940837572));
#153975=CARTESIAN_POINT('Ctrl Pts',(-21.2521952261608,-18.4882062515499,
9.78988326142308));
#153976=CARTESIAN_POINT('Ctrl Pts',(-21.2415125421986,-18.4362666864387,
9.79253711447044));
#153977=CARTESIAN_POINT('Ctrl Pts',(-21.2246679295087,-18.3543676186888,
9.79672174886349));
#153978=CARTESIAN_POINT('Ctrl Pts',(-21.2037753333229,-18.2731422629634,
9.80090638325654));
#153979=CARTESIAN_POINT('Ctrl Pts',(-21.1789030820534,-18.1930211337819,
9.80509101764958));
#153980=CARTESIAN_POINT('Ctrl Pts',(-21.1540662333551,-18.1130140471107,
9.80926969573353));
#153981=CARTESIAN_POINT('Ctrl Pts',(-21.125261116367,-18.0341085006255,
9.81344837381748));
#153982=CARTESIAN_POINT('Ctrl Pts',(-21.0926070466711,-17.9567247619913,
9.81762705190143));
#153983=CARTESIAN_POINT('Ctrl Pts',(-21.059367676244,-17.8779539754568,
9.82188062978687));
#153984=CARTESIAN_POINT('Ctrl Pts',(-21.022140108072,-17.8007605624569,
9.8261342076723));
#153985=CARTESIAN_POINT('Ctrl Pts',(-20.9811033321017,-17.7255716022296,
9.83038778555774));
#153986=CARTESIAN_POINT('Ctrl Pts',(-20.9408621341102,-17.6518403267155,
9.83455889953569));
#153987=CARTESIAN_POINT('Ctrl Pts',(-20.8969583386824,-17.5800368994828,
9.83873001351364));
#153988=CARTESIAN_POINT('Ctrl Pts',(-20.8496085018329,-17.5105421730164,
9.84290112749159));
#153989=CARTESIAN_POINT('Ctrl Pts',(-20.8022745536785,-17.4410707661766,
9.84707084181197));
#153990=CARTESIAN_POINT('Ctrl Pts',(-20.7514971194517,-17.3739069013821,
9.85124055613235));
#153991=CARTESIAN_POINT('Ctrl Pts',(-20.69753660511,-17.3094032751789,9.85541027045272));
#153992=CARTESIAN_POINT('Ctrl Pts',(-20.643578010915,-17.2449019442916,
9.85957983639677));
#153993=CARTESIAN_POINT('Ctrl Pts',(-20.5864368576392,-17.1830610160831,
9.86374940234081));
#153994=CARTESIAN_POINT('Ctrl Pts',(-20.5264135623406,-17.1241997862082,
9.86791896828485));
#153995=CARTESIAN_POINT('Ctrl Pts',(-20.4642799220261,-17.063269068104,
9.87223513102377));
#153996=CARTESIAN_POINT('Ctrl Pts',(-20.3990580731256,-17.0055318485508,
9.87655129376269));
#153997=CARTESIAN_POINT('Ctrl Pts',(-20.3311209857106,-16.9512989836053,
9.88086745650161));
#153998=CARTESIAN_POINT('Ctrl Pts',(-20.2653969417724,-16.8988327485311,
9.88504302069329));
#153999=CARTESIAN_POINT('Ctrl Pts',(-20.1971322502977,-16.84964630251,9.88921858488496));
#154000=CARTESIAN_POINT('Ctrl Pts',(-20.1266949702185,-16.8039774861682,
9.89339414907664));
#154001=CARTESIAN_POINT('Ctrl Pts',(-20.0527000705712,-16.7560020464804,
9.89778061108918));
#154002=CARTESIAN_POINT('Ctrl Pts',(-19.9763078452048,-16.7119092180967,
9.90216707310172));
#154003=CARTESIAN_POINT('Ctrl Pts',(-19.8979731420051,-16.6719196231951,
9.90655353511426));
#154004=CARTESIAN_POINT('Ctrl Pts',(-19.8196384388055,-16.6319300282936,
9.9109399971268));
#154005=CARTESIAN_POINT('Ctrl Pts',(-19.7393618185146,-16.5960438342244,
9.91532645913934));
#154006=CARTESIAN_POINT('Ctrl Pts',(-19.6576188802165,-16.5644221134992,
9.91971292115188));
#154007=CARTESIAN_POINT('Ctrl Pts',(-19.5796370556816,-16.5342553550192,
9.92389755554493));
#154008=CARTESIAN_POINT('Ctrl Pts',(-19.5000306196518,-16.5078569775931,
9.92808218993798));
#154009=CARTESIAN_POINT('Ctrl Pts',(-19.4191985515812,-16.4854025571831,
9.93226682433103));
#154010=CARTESIAN_POINT('Ctrl Pts',(-19.3384815379545,-16.4629800978612,
9.93644550241497));
#154011=CARTESIAN_POINT('Ctrl Pts',(-19.2565427969406,-16.4444905669892,
9.94062418049891));
#154012=CARTESIAN_POINT('Ctrl Pts',(-19.1738002903985,-16.4300611219609,
9.94480285858285));
#154013=CARTESIAN_POINT('Ctrl Pts',(-19.0895746838926,-16.4153730395006,
9.94905643646829));
#154014=CARTESIAN_POINT('Ctrl Pts',(-19.0045166631073,-16.404892202575,
9.95331001435372));
#154015=CARTESIAN_POINT('Ctrl Pts',(-18.9190822179583,-16.3986992788558,
9.95756359223916));
#154016=CARTESIAN_POINT('Ctrl Pts',(-18.8353040862402,-16.3926264170474,
9.96173470621711));
#154017=CARTESIAN_POINT('Ctrl Pts',(-18.7511644753125,-16.3906767277746,
9.96590582019506));
#154018=CARTESIAN_POINT('Ctrl Pts',(-18.6671008395072,-16.3928742699263,
9.97007693417301));
#154019=CARTESIAN_POINT('Ctrl Pts',(-18.5830654120668,-16.3950710746715,
9.97424664849338));
#154020=CARTESIAN_POINT('Ctrl Pts',(-18.4991063686099,-16.4014123350032,
9.97841636281375));
#154021=CARTESIAN_POINT('Ctrl Pts',(-18.4156612239222,-16.4118699986723,
9.98258607713413));
#154022=CARTESIAN_POINT('Ctrl Pts',(-18.3322190485708,-16.4223272902127,
9.98675564307817));
#154023=CARTESIAN_POINT('Ctrl Pts',(-18.2492911919861,-16.4369006358009,
9.99092520902222));
#154024=CARTESIAN_POINT('Ctrl Pts',(-18.1673087413395,-16.4555102609148,
9.99509477496626));
#154025=CARTESIAN_POINT('Ctrl Pts',(-18.0824438888645,-16.4747741774902,
9.99941093770518));
#154026=CARTESIAN_POINT('Ctrl Pts',(-17.9985926745536,-16.498363368963,
10.0037271004441));
#154027=CARTESIAN_POINT('Ctrl Pts',(-17.9162183607824,-16.5261324870145,
10.008043263183));
#154028=CARTESIAN_POINT('Ctrl Pts',(-17.836527381618,-16.5529970289662,
10.0122188273747));
#154029=CARTESIAN_POINT('Ctrl Pts',(-17.7582189816851,-16.5837731410384,
10.0163943915664));
#154030=CARTESIAN_POINT('Ctrl Pts',(-17.6816923706303,-16.6182800825355,
10.0205699557581));
#154031=CARTESIAN_POINT('Ctrl Pts',(-17.6013005823759,-16.6545298876153,
10.0249564177706));
#154032=CARTESIAN_POINT('Ctrl Pts',(-17.5228758288488,-16.6948970480992,
10.0293428797831));
#154033=CARTESIAN_POINT('Ctrl Pts',(-17.4468498189204,-16.7391185274971,
10.0337293417957));
#154034=CARTESIAN_POINT('Ctrl Pts',(-17.3708238089919,-16.7833400068949,
10.0381158038082));
#154035=CARTESIAN_POINT('Ctrl Pts',(-17.2971969868961,-16.8314154242948,
10.0425022658208));
#154036=CARTESIAN_POINT('Ctrl Pts',(-17.2263622218887,-16.8830320616279,
10.0468887278333));
#154037=CARTESIAN_POINT('Ctrl Pts',(-17.1587866694216,-16.9322737409631,
10.0510733622264));
#154038=CARTESIAN_POINT('Ctrl Pts',(-17.0935003576726,-16.9849212146566,
10.0552579966194));
#154039=CARTESIAN_POINT('Ctrl Pts',(-17.0308668782516,-17.0407340400657,
10.0594426310125));
#154040=CARTESIAN_POINT('Ctrl Pts',(-16.9683225498361,-17.0964674228261,
10.0636213090964));
#154041=CARTESIAN_POINT('Ctrl Pts',(-16.9084238939848,-17.1553569045525,
10.0677999871804));
#154042=CARTESIAN_POINT('Ctrl Pts',(-16.8515040647696,-17.2171198733512,
10.0719786652643));
#154043=CARTESIAN_POINT('Ctrl Pts',(-16.7935639885233,-17.2799898989772,
10.0762322431497));
#154044=CARTESIAN_POINT('Ctrl Pts',(-16.7387109698991,-17.345837155491,
10.0804858210352));
#154045=CARTESIAN_POINT('Ctrl Pts',(-16.687259656336,-17.4143218914161,
10.0847393989206));
#154046=CARTESIAN_POINT('Ctrl Pts',(-16.6368058268853,-17.4814789170983,
10.0889105128986));
#154047=CARTESIAN_POINT('Ctrl Pts',(-16.5896232711907,-17.5511716846818,
10.0930816268765));
#154048=CARTESIAN_POINT('Ctrl Pts',(-16.5459690047032,-17.6230453869223,
10.0972527408545));
#154049=CARTESIAN_POINT('Ctrl Pts',(-16.5023293868265,-17.6948949712479,
10.1014224551748));
#154050=CARTESIAN_POINT('Ctrl Pts',(-16.4622159454253,-17.7689236439344,
10.1055921694952));
#154051=CARTESIAN_POINT('Ctrl Pts',(-16.4258419114526,-17.8447483401352,
10.1097618838156));
#154052=CARTESIAN_POINT('Ctrl Pts',(-16.3894691718242,-17.9205703381678,
10.1139314497596));
#154053=CARTESIAN_POINT('Ctrl Pts',(-16.3568357732638,-17.9981878174993,
10.1181010157037));
#154054=CARTESIAN_POINT('Ctrl Pts',(-16.3281079773328,-18.0771951216036,
10.1222705816477));
#154055=CARTESIAN_POINT('Ctrl Pts',(-16.2983701475363,-18.1589802250542,
10.1265867443867));
#154056=CARTESIAN_POINT('Ctrl Pts',(-16.2728178525521,-18.2422542084871,
10.1309029071256));
#154057=CARTESIAN_POINT('Ctrl Pts',(-16.2515796325832,-18.3265488672692,
10.1352190698645));
#154058=CARTESIAN_POINT('Ctrl Pts',(-16.231033245396,-18.4080976364077,
10.1393946340562));
#154059=CARTESIAN_POINT('Ctrl Pts',(-16.2145242335759,-18.4906011339278,
10.1435701982479));
#154060=CARTESIAN_POINT('Ctrl Pts',(-16.2021167074112,-18.5736258561826,
10.1477457624395));
#154061=CARTESIAN_POINT('Ctrl Pts',(-16.189082506596,-18.660843959786,10.1521322244521));
#154062=CARTESIAN_POINT('Ctrl Pts',(-16.1805750686802,-18.7486367448621,
10.1565186864646));
#154063=CARTESIAN_POINT('Ctrl Pts',(-16.176606897426,-18.8364988359063,
10.1609051484772));
#154064=CARTESIAN_POINT('Ctrl Pts',(-16.1726387261718,-18.9243609269505,
10.1652916104897));
#154065=CARTESIAN_POINT('Ctrl Pts',(-16.173209741748,-19.0122917442521,
10.1696780725022));
#154066=CARTESIAN_POINT('Ctrl Pts',(-16.1782696504243,-19.0997916785801,
10.1740645345148));
#154067=CARTESIAN_POINT('Ctrl Pts',(-16.1830972264459,-19.1832739332768,
10.1782495861009));
#154068=CARTESIAN_POINT('Ctrl Pts',(-16.192028478113,-19.2666747744999,
10.1824346376871));
#154069=CARTESIAN_POINT('Ctrl Pts',(-16.2050580322525,-19.3495582017334,
10.1866196892733));
#154070=CARTESIAN_POINT('Ctrl Pts',(-16.218065180498,-19.4322991008905,
10.1907975441571));
#154071=CARTESIAN_POINT('Ctrl Pts',(-16.2351565463996,-19.5145239047392,
10.1949753990409));
#154072=CARTESIAN_POINT('Ctrl Pts',(-16.2562748618458,-19.5957997668208,
10.1991532539248));
#154073=CARTESIAN_POINT('Ctrl Pts',(-16.2773725113785,-19.6769960941531,
10.2033270204528));
#154074=CARTESIAN_POINT('Ctrl Pts',(-16.3024891716641,-19.7572448807793,
10.2075007869809));
#154075=CARTESIAN_POINT('Ctrl Pts',(-16.3315163412368,-19.8361223158454,
10.211674553509));
#154076=CARTESIAN_POINT('Ctrl Pts',(-16.3605238139077,-19.9149462272259,
10.2158454878535));
#154077=CARTESIAN_POINT('Ctrl Pts',(-16.3934363672028,-19.9924002048188,
10.2200164221981));
#154078=CARTESIAN_POINT('Ctrl Pts',(-16.4300957454804,-20.0680757976081,
10.2241873565427));
#154079=CARTESIAN_POINT('Ctrl Pts',(-16.4667412452146,-20.1437227410571,
10.2283567118509));
#154080=CARTESIAN_POINT('Ctrl Pts',(-16.5071305503819,-20.2175922243166,
10.2325260671591));
#154081=CARTESIAN_POINT('Ctrl Pts',(-16.5510579279926,-20.2892972408032,
10.2366954224672));
#154082=CARTESIAN_POINT('Ctrl Pts',(-16.5950001276811,-20.3610264521632,
10.240866184609));
#154083=CARTESIAN_POINT('Ctrl Pts',(-16.6424825511957,-20.4305893408586,
10.2450369467507));
#154084=CARTESIAN_POINT('Ctrl Pts',(-16.6932547035596,-20.497625645186,
10.2492077088924));
#154085=CARTESIAN_POINT('Ctrl Pts',(-16.7440345632818,-20.5646721258164,
10.2533791041678));
#154086=CARTESIAN_POINT('Ctrl Pts',(-16.7981048585996,-20.6291908988194,
10.2575504994432));
#154087=CARTESIAN_POINT('Ctrl Pts',(-16.8551743953647,-20.6908543203405,
10.2617218947185));
#154088=CARTESIAN_POINT('Ctrl Pts',(-16.9123064332259,-20.7525852740627,
10.2658978583993));
#154089=CARTESIAN_POINT('Ctrl Pts',(-16.9724439504671,-20.8114543015288,
10.27007382208));
#154090=CARTESIAN_POINT('Ctrl Pts',(-17.0352588291791,-20.8671706019459,
10.2742497857607));
#154091=CARTESIAN_POINT('Ctrl Pts',(-17.0803268259774,-20.9071455585216,
10.2772459281023));
#154092=CARTESIAN_POINT('Ctrl Pts',(-17.1267722730037,-20.9454983787039,
10.2802420704439));
#154093=CARTESIAN_POINT('Ctrl Pts',(-17.1744641402401,-20.9821349467765,
10.2832382127855));
#154094=CARTESIAN_POINT('Origin',(-18.734,-18.952,-1.76670989022851));
#154095=CARTESIAN_POINT('',(-17.1757180887844,-20.9805344762227,11.1497835108638));
#154096=CARTESIAN_POINT('',(-17.1731949481218,-20.9838169785964,11.0834063298428));
#154097=CARTESIAN_POINT('',(-17.1744641402401,-20.9821349467765,-1.76670989022851));
#154098=CARTESIAN_POINT('',(-21.2939995125392,-18.9504201902087,10.6332901097715));
#154099=CARTESIAN_POINT('Ctrl Pts',(-21.2907951936029,-18.9504028914923,
10.633291065733));
#154100=CARTESIAN_POINT('Ctrl Pts',(-21.2926071610387,-18.6273578228792,
10.6493117789394));
#154101=CARTESIAN_POINT('Ctrl Pts',(-21.0857645521851,-17.4517521226135,
10.7077244277063));
#154102=CARTESIAN_POINT('Ctrl Pts',(-19.3189847766872,-15.9819690623319,
10.8085290120338));
#154103=CARTESIAN_POINT('Ctrl Pts',(-16.553315163514,-16.8524989631863,
10.9357048187152));
#154104=CARTESIAN_POINT('Ctrl Pts',(-15.869042517464,-19.3539801303507,
11.0494563183253));
#154105=CARTESIAN_POINT('Ctrl Pts',(-16.7160809834605,-20.6211555874542,
11.1208158823748));
#154106=CARTESIAN_POINT('Ctrl Pts',(-17.1757180887841,-20.9805344762225,
11.1497835108638));
#154107=CARTESIAN_POINT('Ctrl Pts',(-17.1744641402401,-20.9821349467765,
10.3499274704374));
#154108=CARTESIAN_POINT('Ctrl Pts',(-17.2411279928465,-21.0333456649873,
10.3540972012588));
#154109=CARTESIAN_POINT('Ctrl Pts',(-17.3103427550984,-21.0812892113262,
10.3582669320803));
#154110=CARTESIAN_POINT('Ctrl Pts',(-17.3817509985227,-21.1257117191577,
10.3624366629017));
#154111=CARTESIAN_POINT('Ctrl Pts',(-17.453156251782,-21.1701323668311,
10.366606219119));
#154112=CARTESIAN_POINT('Ctrl Pts',(-17.526754412567,-21.2110320268083,
10.3707757753362));
#154113=CARTESIAN_POINT('Ctrl Pts',(-17.6021604511976,-21.2482010442831,
10.3749453315534));
#154114=CARTESIAN_POINT('Ctrl Pts',(-17.6806131725609,-21.2868718274757,
10.3792833532564));
#154115=CARTESIAN_POINT('Ctrl Pts',(-17.7610224891159,-21.321503848979,
10.3836213749594));
#154116=CARTESIAN_POINT('Ctrl Pts',(-17.8429301077372,-21.3519155083258,
10.3879593966624));
#154117=CARTESIAN_POINT('Ctrl Pts',(-17.9217695912436,-21.3811879930572,
10.3921349226545));
#154118=CARTESIAN_POINT('Ctrl Pts',(-18.0019966600383,-21.4065505716589,
10.3963104486466));
#154119=CARTESIAN_POINT('Ctrl Pts',(-18.0831873454017,-21.427892341887,
10.4004859746387));
#154120=CARTESIAN_POINT('Ctrl Pts',(-18.1644360817491,-21.4492493713872,
10.4046644861136));
#154121=CARTESIAN_POINT('Ctrl Pts',(-18.2466493563219,-21.4665797778481,
10.4088429975885));
#154122=CARTESIAN_POINT('Ctrl Pts',(-18.3293941447886,-21.4798239855513,
10.4130215090634));
#154123=CARTESIAN_POINT('Ctrl Pts',(-18.4122671639293,-21.4930887179754,
10.4172064960318));
#154124=CARTESIAN_POINT('Ctrl Pts',(-18.4956728843019,-21.5022545728989,
10.4213914830002));
#154125=CARTESIAN_POINT('Ctrl Pts',(-18.5791750022087,-21.5073139181046,
10.4255764699687));
#154126=CARTESIAN_POINT('Ctrl Pts',(-18.5886533835364,-21.5078882077673,
10.4260515106423));
#154127=CARTESIAN_POINT('Ctrl Pts',(-18.5981330099311,-21.5084096415651,
10.4265265513159));
#154128=CARTESIAN_POINT('Ctrl Pts',(-18.607613246377,-21.5088782506229,
10.4270015919895));
#154129=CARTESIAN_POINT('Ctrl Pts',(-18.6911246711664,-21.5130062288976,
10.4311862263825));
#154130=CARTESIAN_POINT('Ctrl Pts',(-18.7749939587053,-21.5130461767751,
10.4353708607756));
#154131=CARTESIAN_POINT('Ctrl Pts',(-18.8587871646377,-21.5089568169098,
10.4395554951686));
#154132=CARTESIAN_POINT('Ctrl Pts',(-18.9424611013132,-21.5048732777422,
10.4437341732526));
#154133=CARTESIAN_POINT('Ctrl Pts',(-19.0260587159297,-21.496672127745,
10.4479128513366));
#154134=CARTESIAN_POINT('Ctrl Pts',(-19.1091432618602,-21.4843640206497,
10.4520915294205));
#154135=CARTESIAN_POINT('Ctrl Pts',(-19.1937170385644,-21.4718352995804,
10.4563451073059));
#154136=CARTESIAN_POINT('Ctrl Pts',(-19.2777586906012,-21.4550509150071,
10.4605986851914));
#154137=CARTESIAN_POINT('Ctrl Pts',(-19.3608099823642,-21.4340776067659,
10.4648522630768));
#154138=CARTESIAN_POINT('Ctrl Pts',(-19.4422511627753,-21.4135109070309,
10.4690233770548));
#154139=CARTESIAN_POINT('Ctrl Pts',(-19.5227395737981,-21.388916372956,
10.4731944910327));
#154140=CARTESIAN_POINT('Ctrl Pts',(-19.6018523684388,-21.3604086585535,
10.4773656050107));
#154141=CARTESIAN_POINT('Ctrl Pts',(-19.6809386160172,-21.3319105101898,
10.481535319331));
#154142=CARTESIAN_POINT('Ctrl Pts',(-19.7586497315295,-21.2995019451702,
10.4857050336514));
#154143=CARTESIAN_POINT('Ctrl Pts',(-19.834579189332,-21.2633471067776,
10.4898747479718));
#154144=CARTESIAN_POINT('Ctrl Pts',(-19.9105059452386,-21.2271935549294,
10.4940443139158));
#154145=CARTESIAN_POINT('Ctrl Pts',(-19.9846507545054,-21.1872941933034,
10.4982138798599));
#154146=CARTESIAN_POINT('Ctrl Pts',(-20.0566294498849,-21.1438602460689,
10.5023834458039));
#154147=CARTESIAN_POINT('Ctrl Pts',(-20.1311388273984,-21.0988992148313,
10.5066996085428));
#154148=CARTESIAN_POINT('Ctrl Pts',(-20.203326484239,-21.0501506938732,
10.5110157712818));
#154149=CARTESIAN_POINT('Ctrl Pts',(-20.2727983186254,-20.9978982708326,
10.5153319340207));
#154150=CARTESIAN_POINT('Ctrl Pts',(-20.3400071153138,-20.9473479649765,
10.5195074982123));
#154151=CARTESIAN_POINT('Ctrl Pts',(-20.4046739763899,-20.8935188682638,
10.523683062404));
#154152=CARTESIAN_POINT('Ctrl Pts',(-20.4664767307277,-20.8367080350778,
10.5278586265957));
#154153=CARTESIAN_POINT('Ctrl Pts',(-20.5314009952649,-20.7770278217627,
10.5322450886082));
#154154=CARTESIAN_POINT('Ctrl Pts',(-20.5931638083648,-20.7140571577257,
10.5366315506208));
#154155=CARTESIAN_POINT('Ctrl Pts',(-20.6514380125593,-20.6481814372268,
10.5410180126333));
#154156=CARTESIAN_POINT('Ctrl Pts',(-20.7097122167537,-20.5823057167279,
10.5454044746458));
#154157=CARTESIAN_POINT('Ctrl Pts',(-20.7644975100436,-20.5135254409999,
10.5497909366584));
#154158=CARTESIAN_POINT('Ctrl Pts',(-20.8155192213965,-20.4422609606901,
10.5541773986709));
#154159=CARTESIAN_POINT('Ctrl Pts',(-20.8646271615163,-20.3736695367859,
10.5583993290636));
#154160=CARTESIAN_POINT('Ctrl Pts',(-20.9104308246501,-20.302523084569,
10.5626212594563));
#154161=CARTESIAN_POINT('Ctrl Pts',(-20.9526566798058,-20.2291697370174,
10.5668431898491));
#154162=CARTESIAN_POINT('Ctrl Pts',(-20.9948201353165,-20.1559247880485,
10.5710588812454));
#154163=CARTESIAN_POINT('Ctrl Pts',(-21.0334160638335,-20.0804798079433,
10.5752745726417));
#154164=CARTESIAN_POINT('Ctrl Pts',(-21.0682129788551,-20.003213474678,
10.5794902640381));
#154165=CARTESIAN_POINT('Ctrl Pts',(-21.1029682787105,-19.9260395476302,
10.583700913703));
#154166=CARTESIAN_POINT('Ctrl Pts',(-21.1339334100815,-19.8470490030809,
10.587911563368));
#154167=CARTESIAN_POINT('Ctrl Pts',(-21.1609223976385,-19.7666457364035,
10.592122213033));
#154168=CARTESIAN_POINT('Ctrl Pts',(-21.1878844462892,-19.6863227237952,
10.5963286598616));
#154169=CARTESIAN_POINT('Ctrl Pts',(-21.2108781024615,-19.6045902181226,
10.6005351066903));
#154170=CARTESIAN_POINT('Ctrl Pts',(-21.2297657078558,-19.5218715043685,
10.6047415535189));
#154171=CARTESIAN_POINT('Ctrl Pts',(-21.24864245849,-19.4392003292924,10.6089455828907));
#154172=CARTESIAN_POINT('Ctrl Pts',(-21.2634177498248,-19.3555445100527,
10.6131496122625));
#154173=CARTESIAN_POINT('Ctrl Pts',(-21.27400421321,-19.2713408788045,10.6173536416343));
#154174=CARTESIAN_POINT('Ctrl Pts',(-21.2845883389273,-19.1871558411237,
10.6215567426863));
#154175=CARTESIAN_POINT('Ctrl Pts',(-21.2909854180498,-19.1024236771956,
10.6257598437382));
#154176=CARTESIAN_POINT('Ctrl Pts',(-21.2931596531403,-19.0175886403171,
10.6299629447901));
#154177=CARTESIAN_POINT('Ctrl Pts',(-21.2937333596144,-18.99520356793,10.6310719997839));
#154178=CARTESIAN_POINT('Ctrl Pts',(-21.2940133304248,-18.9728113543426,
10.6321810547777));
#154179=CARTESIAN_POINT('Ctrl Pts',(-21.2939995125392,-18.9504201902087,
10.6332901097715));
#154180=CARTESIAN_POINT('',(-21.2940195635259,-18.9533010451044,10.566709896691));
#154181=CARTESIAN_POINT('Ctrl Pts',(-17.1744641402401,-20.9821349467765,
10.2832382127855));
#154182=CARTESIAN_POINT('Ctrl Pts',(-17.2410685654238,-21.0333000132453,
10.2874224972348));
#154183=CARTESIAN_POINT('Ctrl Pts',(-17.3101047703225,-21.0811157710451,
10.291606781684));
#154184=CARTESIAN_POINT('Ctrl Pts',(-17.3811935362982,-21.125364827121,
10.2957910661332));
#154185=CARTESIAN_POINT('Ctrl Pts',(-17.4120536307295,-21.1445736293875,
10.2976074911542));
#154186=CARTESIAN_POINT('Ctrl Pts',(-17.443300225641,-21.1631108865338,
10.2994239161752));
#154187=CARTESIAN_POINT('Ctrl Pts',(-17.4749010481802,-21.1809616034213,
10.3012403411962));
#154188=CARTESIAN_POINT('Ctrl Pts',(-17.5477022303472,-21.2220856371494,
10.3054249755892));
#154189=CARTESIAN_POINT('Ctrl Pts',(-17.622655768781,-21.2597157589185,
10.3096096099823));
#154190=CARTESIAN_POINT('Ctrl Pts',(-17.6993922596291,-21.2936205549928,
10.3137942443753));
#154191=CARTESIAN_POINT('Ctrl Pts',(-17.7760195255806,-21.3274770917864,
10.3179729224593));
#154192=CARTESIAN_POINT('Ctrl Pts',(-17.8544242858622,-21.3576186510691,
10.3221516005432));
#154193=CARTESIAN_POINT('Ctrl Pts',(-17.9342113535407,-21.3838589846031,
10.3263302786272));
#154194=CARTESIAN_POINT('Ctrl Pts',(-18.0154285470654,-21.4105696572571,
10.3305838565126));
#154195=CARTESIAN_POINT('Ctrl Pts',(-18.098077671342,-21.43323763244,10.334837434398));
#154196=CARTESIAN_POINT('Ctrl Pts',(-18.1817191896633,-21.4517171653077,
10.3390910122835));
#154197=CARTESIAN_POINT('Ctrl Pts',(-18.2637391539389,-21.4698384363709,
10.3432621262614));
#154198=CARTESIAN_POINT('Ctrl Pts',(-18.3467129067618,-21.4839321143086,
10.3474332402394));
#154199=CARTESIAN_POINT('Ctrl Pts',(-18.4302110680644,-21.4939111480997,
10.3516043542173));
#154200=CARTESIAN_POINT('Ctrl Pts',(-18.5136812107526,-21.5038868333296,
10.3557740685377));
#154201=CARTESIAN_POINT('Ctrl Pts',(-18.5976749560384,-21.5097505619763,
10.3599437828581));
#154202=CARTESIAN_POINT('Ctrl Pts',(-18.6817553300755,-21.5114668379302,
10.3641134971784));
#154203=CARTESIAN_POINT('Ctrl Pts',(-18.765832712172,-21.5131830528116,
10.3682830631225));
#154204=CARTESIAN_POINT('Ctrl Pts',(-18.8499962569364,-21.510752099899,
10.3724526290665));
#154205=CARTESIAN_POINT('Ctrl Pts',(-18.9338078728664,-21.5041905912256,
10.3766221950106));
#154206=CARTESIAN_POINT('Ctrl Pts',(-19.0205662018199,-21.4973983880018,
10.3809383577495));
#154207=CARTESIAN_POINT('Ctrl Pts',(-19.1069468680351,-21.4861798052051,
10.3852545204884));
#154208=CARTESIAN_POINT('Ctrl Pts',(-19.1924704625207,-21.4706116880131,
10.3895706832273));
#154209=CARTESIAN_POINT('Ctrl Pts',(-19.2752081349114,-21.4555507006011,
10.393746247419));
#154210=CARTESIAN_POINT('Ctrl Pts',(-19.3571432683312,-21.4364193523527,
10.3979218116107));
#154211=CARTESIAN_POINT('Ctrl Pts',(-19.4378547167232,-21.413338769399,
10.4020973758024));
#154212=CARTESIAN_POINT('Ctrl Pts',(-19.5226427085003,-21.3890924410692,
10.4064838378149));
#154213=CARTESIAN_POINT('Ctrl Pts',(-19.6060795975568,-21.3604876310562,
10.4108702998275));
#154214=CARTESIAN_POINT('Ctrl Pts',(-19.6877001821497,-21.3277221981048,
10.41525676184));
#154215=CARTESIAN_POINT('Ctrl Pts',(-19.7693207667425,-21.2949567651533,
10.4196432238525));
#154216=CARTESIAN_POINT('Ctrl Pts',(-19.8491245522345,-21.2580310219481,
10.4240296858651));
#154217=CARTESIAN_POINT('Ctrl Pts',(-19.9266775857364,-21.2171976020829,
10.4284161478776));
#154218=CARTESIAN_POINT('Ctrl Pts',(-20.0006622892057,-21.1782429883953,
10.4326007822707));
#154219=CARTESIAN_POINT('Ctrl Pts',(-20.0728741952655,-21.1355873954291,
10.4367854166637));
#154220=CARTESIAN_POINT('Ctrl Pts',(-20.1429187702871,-21.0894161734984,
10.4409700510568));
#154221=CARTESIAN_POINT('Ctrl Pts',(-20.212863645526,-21.0433106705873,
10.4451487291407));
#154222=CARTESIAN_POINT('Ctrl Pts',(-20.2806469365542,-20.9936997293726,
10.4493274072247));
#154223=CARTESIAN_POINT('Ctrl Pts',(-20.3458981308864,-20.9408148268869,
10.4535060853086));
#154224=CARTESIAN_POINT('Ctrl Pts',(-20.4123189059818,-20.8869820005318,
10.4577596631941));
#154225=CARTESIAN_POINT('Ctrl Pts',(-20.476115489232,-20.829756911557,10.4620132410795));
#154226=CARTESIAN_POINT('Ctrl Pts',(-20.5369274194047,-20.7694302518553,
10.4662668189649));
#154227=CARTESIAN_POINT('Ctrl Pts',(-20.5965603916463,-20.7102731421696,
10.4704379329429));
#154228=CARTESIAN_POINT('Ctrl Pts',(-20.6533230631004,-20.6481339874866,
10.4746090469208));
#154229=CARTESIAN_POINT('Ctrl Pts',(-20.7069098223475,-20.5833267094254,
10.4787801608988));
#154230=CARTESIAN_POINT('Ctrl Pts',(-20.7604786000401,-20.5185411780722,
10.4829498752192));
#154231=CARTESIAN_POINT('Ctrl Pts',(-20.8108732891326,-20.4510896556873,
10.4871195895395));
#154232=CARTESIAN_POINT('Ctrl Pts',(-20.8578275173592,-20.3813203547519,
10.4912893038599));
#154233=CARTESIAN_POINT('Ctrl Pts',(-20.9047800747528,-20.3115535365075,
10.4954588698039));
#154234=CARTESIAN_POINT('Ctrl Pts',(-20.948292158553,-20.2394694858254,
10.499628435748));
#154235=CARTESIAN_POINT('Ctrl Pts',(-20.9881406062299,-20.1654455601079,
10.503798001692));
#154236=CARTESIAN_POINT('Ctrl Pts',(-21.0293900761687,-20.0888190444805,
10.508114164431));
#154237=CARTESIAN_POINT('Ctrl Pts',(-21.0667132396993,-20.0101141681398,
10.5124303271699));
#154238=CARTESIAN_POINT('Ctrl Pts',(-21.0999152164605,-19.9297756330163,
10.5167464899088));
#154239=CARTESIAN_POINT('Ctrl Pts',(-21.132035642321,-19.8520541172245,
10.5209220541005));
#154240=CARTESIAN_POINT('Ctrl Pts',(-21.160299139743,-19.7728042005822,
10.5250976182921));
#154241=CARTESIAN_POINT('Ctrl Pts',(-21.1845795982613,-19.6924455635532,
10.5292731824838));
#154242=CARTESIAN_POINT('Ctrl Pts',(-21.210086405018,-19.6080282028024,
10.5336596444964));
#154243=CARTESIAN_POINT('Ctrl Pts',(-21.231197092147,-19.522387742153,10.5380461065089));
#154244=CARTESIAN_POINT('Ctrl Pts',(-21.2478262226603,-19.4360224398369,
10.5424325685214));
#154245=CARTESIAN_POINT('Ctrl Pts',(-21.2644553531735,-19.3496571375209,
10.546819030534));
#154246=CARTESIAN_POINT('Ctrl Pts',(-21.2766029222518,-19.2625675787001,
10.5512054925465));
#154247=CARTESIAN_POINT('Ctrl Pts',(-21.2842464642989,-19.1752553948527,
10.555591954559));
#154248=CARTESIAN_POINT('Ctrl Pts',(-21.2907042434478,-19.1014881810632,
10.5592979331155));
#154249=CARTESIAN_POINT('Ctrl Pts',(-21.293961988618,-19.0274367677245,
10.563003911672));
#154250=CARTESIAN_POINT('Ctrl Pts',(-21.2939996693303,-18.9533011644427,
10.5667098902285));
#154251=CARTESIAN_POINT('Ctrl Pts',(-21.2974134575541,-18.9532806863302,
10.5667109991706));
#154252=CARTESIAN_POINT('Ctrl Pts',(-21.2925956544959,-18.178366843738,
10.6053965865272));
#154253=CARTESIAN_POINT('Ctrl Pts',(-20.5048167981983,-16.5458335938225,
10.6864741094444));
#154254=CARTESIAN_POINT('Ctrl Pts',(-17.7257693559758,-16.0977467181734,
10.8099435679219));
#154255=CARTESIAN_POINT('Ctrl Pts',(-15.7882885603548,-18.254809249408,
10.9371193746034));
#154256=CARTESIAN_POINT('Ctrl Pts',(-16.3366273719947,-20.2593599478178,
11.028273628577));
#154257=CARTESIAN_POINT('Ctrl Pts',(-17.0711421117158,-20.9069199380455,
11.0770359469901));
#154258=CARTESIAN_POINT('Ctrl Pts',(-17.1731949481218,-20.9838169785965,
11.0834063298428));
#154259=CARTESIAN_POINT('Origin',(-18.734,-18.952,-1.76670989022851));
#154260=CARTESIAN_POINT('',(-17.1744641402401,-20.9821349467765,11.949868723648));
#154261=CARTESIAN_POINT('',(-17.1744641402401,-20.9821349467765,11.8833305046723));
#154262=CARTESIAN_POINT('',(-17.1744641402401,-20.9821349467765,-1.76670989022851));
#154263=CARTESIAN_POINT('',(-21.2940195831445,-18.9506989550129,11.4332901033027));
#154264=CARTESIAN_POINT('Ctrl Pts',(-21.2939996693303,-18.9506988355569,
11.4332901097715));
#154265=CARTESIAN_POINT('Ctrl Pts',(-21.293961988618,-18.8765632322752,
11.436996088328));
#154266=CARTESIAN_POINT('Ctrl Pts',(-21.2907042434478,-18.8025118189363,
11.4407020668845));
#154267=CARTESIAN_POINT('Ctrl Pts',(-21.2842464642989,-18.7287446051466,
11.444408045441));
#154268=CARTESIAN_POINT('Ctrl Pts',(-21.2769546129518,-18.6454497843058,
11.4485926798341));
#154269=CARTESIAN_POINT('Ctrl Pts',(-21.2655641024497,-18.5623575749322,
11.4527773142271));
#154270=CARTESIAN_POINT('Ctrl Pts',(-21.250093180474,-18.4799034980303,
11.4569619486201));
#154271=CARTESIAN_POINT('Ctrl Pts',(-21.2346442794409,-18.3975667843011,
11.4611406267041));
#154272=CARTESIAN_POINT('Ctrl Pts',(-21.2151265874821,-18.3158668471444,
11.465319304788));
#154273=CARTESIAN_POINT('Ctrl Pts',(-21.1916101807317,-18.2352349062881,
11.469497982872));
#154274=CARTESIAN_POINT('Ctrl Pts',(-21.1676722592913,-18.1531576958412,
11.4737515607574));
#154275=CARTESIAN_POINT('Ctrl Pts',(-21.1395909011584,-18.07218762626,11.4780051386429));
#154276=CARTESIAN_POINT('Ctrl Pts',(-21.1074946738889,-17.9927695620858,
11.4822587165283));
#154277=CARTESIAN_POINT('Ctrl Pts',(-21.0760206946157,-17.9148911720574,
11.4864298305062));
#154278=CARTESIAN_POINT('Ctrl Pts',(-21.0406863094724,-17.8385055933015,
11.4906009444842));
#154279=CARTESIAN_POINT('Ctrl Pts',(-21.0016627302193,-17.7640161019717,
11.4947720584621));
#154280=CARTESIAN_POINT('Ctrl Pts',(-20.962652245705,-17.6895516063101,
11.4989417727825));
#154281=CARTESIAN_POINT('Ctrl Pts',(-20.9199552389621,-17.6169823416316,
11.5031114871029));
#154282=CARTESIAN_POINT('Ctrl Pts',(-20.8737897249261,-17.5466886704004,
11.5072812014233));
#154283=CARTESIAN_POINT('Ctrl Pts',(-20.8276258536571,-17.4763975005198,
11.5114507673673));
#154284=CARTESIAN_POINT('Ctrl Pts',(-20.7779939737416,-17.4083821471397,
11.5156203333113));
#154285=CARTESIAN_POINT('Ctrl Pts',(-20.725155694621,-17.3429944065422,
11.5197898992554));
#154286=CARTESIAN_POINT('Ctrl Pts',(-20.6704596867895,-17.2753077136497,
11.5241060619943));
#154287=CARTESIAN_POINT('Ctrl Pts',(-20.6123279420988,-17.2104372553888,
11.5284222247332));
#154288=CARTESIAN_POINT('Ctrl Pts',(-20.5510951122123,-17.1487348078626,
11.5327383874721));
#154289=CARTESIAN_POINT('Ctrl Pts',(-20.4918569353188,-17.0890423110747,
11.5369139516638));
#154290=CARTESIAN_POINT('Ctrl Pts',(-20.4297169860238,-17.0323148814138,
11.5410895158555));
#154291=CARTESIAN_POINT('Ctrl Pts',(-20.3650134540526,-16.9788312001506,
11.5452650800472));
#154292=CARTESIAN_POINT('Ctrl Pts',(-20.2970419004996,-16.9226461852921,
11.5496515420597));
#154293=CARTESIAN_POINT('Ctrl Pts',(-20.2262414538865,-16.8700415621995,
11.5540380040722));
#154294=CARTESIAN_POINT('Ctrl Pts',(-20.1530384991427,-16.8212889126043,
11.5584244660848));
#154295=CARTESIAN_POINT('Ctrl Pts',(-20.0798355443989,-16.7725362630091,
11.5628109280973));
#154296=CARTESIAN_POINT('Ctrl Pts',(-20.0042306192382,-16.7276358177823,
11.5671973901099));
#154297=CARTESIAN_POINT('Ctrl Pts',(-19.9266775857363,-16.6868023979171,
11.5715838521224));
#154298=CARTESIAN_POINT('Ctrl Pts',(-19.852692882267,-16.6478477842295,
11.5757684865155));
#154299=CARTESIAN_POINT('Ctrl Pts',(-19.7766600165143,-16.6124491640088,
11.5799531209085));
#154300=CARTESIAN_POINT('Ctrl Pts',(-19.6989550698441,-16.5808269331021,
11.5841377553016));
#154301=CARTESIAN_POINT('Ctrl Pts',(-19.6213607265476,-16.549249712527,
11.5883164333855));
#154302=CARTESIAN_POINT('Ctrl Pts',(-19.5420994522192,-16.5214383763015,
11.5924951114694));
#154303=CARTESIAN_POINT('Ctrl Pts',(-19.4615717652903,-16.4975674125468,
11.5966737895534));
#154304=CARTESIAN_POINT('Ctrl Pts',(-19.3796006774474,-16.4732685789225,
11.6009273674388));
#154305=CARTESIAN_POINT('Ctrl Pts',(-19.2963177561687,-16.4530529941954,
11.6051809453242));
#154306=CARTESIAN_POINT('Ctrl Pts',(-19.2121666533115,-16.4370533501363,
11.6094345232097));
#154307=CARTESIAN_POINT('Ctrl Pts',(-19.1296469837906,-16.4213638903979,
11.6136056371876));
#154308=CARTESIAN_POINT('Ctrl Pts',(-19.0462929678283,-16.4097284515022,
11.6177767511656));
#154309=CARTESIAN_POINT('Ctrl Pts',(-18.9625363705284,-16.4022213571869,
11.6219478651435));
#154310=CARTESIAN_POINT('Ctrl Pts',(-18.8788078785636,-16.3947167819496,
11.6261175794639));
#154311=CARTESIAN_POINT('Ctrl Pts',(-18.794677531367,-16.3913378410871,
11.6302872937843));
#154312=CARTESIAN_POINT('Ctrl Pts',(-18.7105831609267,-16.3921071015279,
11.6344570081047));
#154313=CARTESIAN_POINT('Ctrl Pts',(-18.626491782925,-16.3928763345952,
11.6386265740487));
#154314=CARTESIAN_POINT('Ctrl Pts',(-18.5424368391401,-16.3977934704174,
11.6427961399927));
#154315=CARTESIAN_POINT('Ctrl Pts',(-18.458855738801,-16.4068289575101,
11.6469657059368));
#154316=CARTESIAN_POINT('Ctrl Pts',(-18.3723360300824,-16.4161821211824,
11.6512818686757));
#154317=CARTESIAN_POINT('Ctrl Pts',(-18.2863246298124,-16.4299485702282,
11.6555980314146));
#154318=CARTESIAN_POINT('Ctrl Pts',(-18.2012984666218,-16.4480373252909,
11.6599141941535));
#154319=CARTESIAN_POINT('Ctrl Pts',(-18.1190420217539,-16.46553684106,11.6640897583452));
#154320=CARTESIAN_POINT('Ctrl Pts',(-18.0377080547433,-16.4870812228023,
11.6682653225369));
#154321=CARTESIAN_POINT('Ctrl Pts',(-17.9577139481205,-16.5125369513646,
11.6724408867286));
#154322=CARTESIAN_POINT('Ctrl Pts',(-17.8736795293402,-16.5392783882614,
11.6768273487411));
#154323=CARTESIAN_POINT('Ctrl Pts',(-17.7911244272665,-16.570336474695,
11.6812138107537));
#154324=CARTESIAN_POINT('Ctrl Pts',(-17.7105077932321,-16.605499690457,
11.6856002727662));
#154325=CARTESIAN_POINT('Ctrl Pts',(-17.6298911591977,-16.640662906219,
11.6899867347788));
#154326=CARTESIAN_POINT('Ctrl Pts',(-17.5512134783828,-16.6799309241434,
11.6943731967913));
#154327=CARTESIAN_POINT('Ctrl Pts',(-17.4749010481801,-16.7230383965788,
11.6987596588038));
#154328=CARTESIAN_POINT('Ctrl Pts',(-17.4020998660131,-16.7641624303069,
11.7029442931969));
#154329=CARTESIAN_POINT('Ctrl Pts',(-17.3311800802061,-16.8089334362055,
11.7071289275899));
#154330=CARTESIAN_POINT('Ctrl Pts',(-17.2625305744984,-16.8571544854539,
11.711313561983));
#154331=CARTESIAN_POINT('Ctrl Pts',(-17.193978782865,-16.9053068980072,
11.7154922400669));
#154332=CARTESIAN_POINT('Ctrl Pts',(-17.1276912258538,-16.9568993375337,
11.7196709181509));
#154333=CARTESIAN_POINT('Ctrl Pts',(-17.0640314133917,-17.0116894785263,
11.7238495962348));
#154334=CARTESIAN_POINT('Ctrl Pts',(-16.9992305445427,-17.0674616934193,
11.7281031741202));
#154335=CARTESIAN_POINT('Ctrl Pts',(-16.9371529712703,-17.1265471378129,
11.7323567520057));
#154336=CARTESIAN_POINT('Ctrl Pts',(-16.8781504066903,-17.188644594243,
11.7366103298911));
#154337=CARTESIAN_POINT('Ctrl Pts',(-16.8202917219588,-17.2495381703071,
11.7407814438691));
#154338=CARTESIAN_POINT('Ctrl Pts',(-16.7653902112893,-17.3133276642816,
11.744952557847));
#154339=CARTESIAN_POINT('Ctrl Pts',(-16.7137420754447,-17.3796902600723,
11.749123671825));
#154340=CARTESIAN_POINT('Ctrl Pts',(-16.6621112706308,-17.4460305872531,
11.7532933861453));
#154341=CARTESIAN_POINT('Ctrl Pts',(-16.6137319548151,-17.5149419387272,
11.7574631004657));
#154342=CARTESIAN_POINT('Ctrl Pts',(-16.5688600933643,-17.5860683821312,
11.7616328147861));
#154343=CARTESIAN_POINT('Ctrl Pts',(-16.5239898286469,-17.6571922945512,
11.7658023807301));
#154344=CARTESIAN_POINT('Ctrl Pts',(-16.4826270148772,-17.7305307526507,
11.7699719466742));
#154345=CARTESIAN_POINT('Ctrl Pts',(-16.4449835652527,-17.8056999688316,
11.7741415126182));
#154346=CARTESIAN_POINT('Ctrl Pts',(-16.4060166183775,-17.8835120419223,
11.7784576753571));
#154347=CARTESIAN_POINT('Ctrl Pts',(-16.3710356838062,-17.9632855357175,
11.7827738380961));
#154348=CARTESIAN_POINT('Ctrl Pts',(-16.34022241472,-18.0445701833138,11.787090000835));
#154349=CARTESIAN_POINT('Ctrl Pts',(-16.3104128846333,-18.1232069920643,
11.7912655650267));
#154350=CARTESIAN_POINT('Ctrl Pts',(-16.2845037664842,-18.2032575521564,
11.7954411292184));
#154351=CARTESIAN_POINT('Ctrl Pts',(-16.262608713042,-18.2842986395491,
11.79961669341));
#154352=CARTESIAN_POINT('Ctrl Pts',(-16.239607792501,-18.3694329196091,
11.8040031554226));
#154353=CARTESIAN_POINT('Ctrl Pts',(-16.2210372171718,-18.4556598489484,
11.8083896174351));
#154354=CARTESIAN_POINT('Ctrl Pts',(-16.2069676619406,-18.5424788620814,
11.8127760794477));
#154355=CARTESIAN_POINT('Ctrl Pts',(-16.1928981067095,-18.6292978752144,
11.8171625414602));
#154356=CARTESIAN_POINT('Ctrl Pts',(-16.1833295591005,-18.7167083870925,
11.8215490034728));
#154357=CARTESIAN_POINT('Ctrl Pts',(-16.1782696504242,-18.8042083214207,
11.8259354654853));
#154358=CARTESIAN_POINT('Ctrl Pts',(-16.1734424727601,-18.8876836874068,
11.8301201717333));
#154359=CARTESIAN_POINT('Ctrl Pts',(-16.1727003261448,-18.9715511471448,
11.8343048779813));
#154360=CARTESIAN_POINT('Ctrl Pts',(-16.176088121868,-19.0553770947132,
11.8384895842293));
#154361=CARTESIAN_POINT('Ctrl Pts',(-16.1794710795846,-19.1390833330277,
11.8426683144272));
#154362=CARTESIAN_POINT('Ctrl Pts',(-16.1869722459993,-19.222747721166,
11.8468470446251));
#154363=CARTESIAN_POINT('Ctrl Pts',(-16.1985846232559,-19.3059334222275,
11.8510257748229));
#154364=CARTESIAN_POINT('Ctrl Pts',(-16.2101833131999,-19.3890210737101,
11.8551995796222));
#154365=CARTESIAN_POINT('Ctrl Pts',(-16.2258835179307,-19.4716307065061,
11.8593733844215));
#154366=CARTESIAN_POINT('Ctrl Pts',(-16.2456263033261,-19.5533288166232,
11.8635471892208));
#154367=CARTESIAN_POINT('Ctrl Pts',(-16.2653562958475,-19.6349739882308,
11.8677182894898));
#154368=CARTESIAN_POINT('Ctrl Pts',(-16.2891235604533,-19.7157083639801,
11.8718893897589));
#154369=CARTESIAN_POINT('Ctrl Pts',(-16.3168179573538,-19.79510792471,11.876060490028));
#154370=CARTESIAN_POINT('Ctrl Pts',(-16.3445027167196,-19.8744798547236,
11.8802301387716));
#154371=CARTESIAN_POINT('Ctrl Pts',(-16.3761117424979,-19.9525174584114,
11.8843997875152));
#154372=CARTESIAN_POINT('Ctrl Pts',(-16.4114852391772,-20.0288125118887,
11.8885694362587));
#154373=CARTESIAN_POINT('Ctrl Pts',(-16.4468570371484,-20.1051039015206,
11.8927388847672));
#154374=CARTESIAN_POINT('Ctrl Pts',(-16.4859927520516,-20.1796524905064,
11.8969083332757));
#154375=CARTESIAN_POINT('Ctrl Pts',(-16.5286852775857,-20.2520719115121,
11.9010777817841));
#154376=CARTESIAN_POINT('Ctrl Pts',(-16.5714158514074,-20.3245558739082,
11.9052509461743));
#154377=CARTESIAN_POINT('Ctrl Pts',(-16.6177093345226,-20.3949064802965,
11.9094241105645));
#154378=CARTESIAN_POINT('Ctrl Pts',(-16.6673139151431,-20.462764252509,
11.9135972749547));
#154379=CARTESIAN_POINT('Ctrl Pts',(-16.7169399758274,-20.5306514088884,
11.9177722464328));
#154380=CARTESIAN_POINT('Ctrl Pts',(-16.7698797015918,-20.59604322183,11.9219472179109));
#154381=CARTESIAN_POINT('Ctrl Pts',(-16.8258408815955,-20.6586132481759,
11.9261221893889));
#154382=CARTESIAN_POINT('Ctrl Pts',(-16.8818951703622,-20.7212873791486,
11.9303041072257));
#154383=CARTESIAN_POINT('Ctrl Pts',(-16.9409806346913,-20.7811300140031,
11.9344860250625));
#154384=CARTESIAN_POINT('Ctrl Pts',(-17.0027682220265,-20.8378516725699,
11.9386679428993));
#154385=CARTESIAN_POINT('Ctrl Pts',(-17.0579318451728,-20.888492461964,
11.9424015364822));
#154386=CARTESIAN_POINT('Ctrl Pts',(-17.1152486151753,-20.9366459831291,
11.9461351300651));
#154387=CARTESIAN_POINT('Ctrl Pts',(-17.1744641402401,-20.9821349467765,
11.949868723648));
#154388=CARTESIAN_POINT('Ctrl Pts',(-17.1757180887841,-20.9805344762225,
11.1497835108638));
#154389=CARTESIAN_POINT('Ctrl Pts',(-17.388725157886,-21.1470794372515,
11.1632078179353));
#154390=CARTESIAN_POINT('Ctrl Pts',(-18.3777720013044,-21.7011259744509,
11.2190240605671));
#154391=CARTESIAN_POINT('Ctrl Pts',(-20.5048168108401,-21.3581664234228,
11.3135258905536));
#154392=CARTESIAN_POINT('Ctrl Pts',(-21.2925956727874,-19.7256331618843,
11.3946034134688));
#154393=CARTESIAN_POINT('Ctrl Pts',(-21.2974134759181,-18.9507193137797,
11.4332890008234));
#154394=CARTESIAN_POINT('',(-21.2939995125392,-18.9535798097909,11.3667098902285));
#154395=CARTESIAN_POINT('Ctrl Pts',(-17.1731949481218,-20.9838169785965,
11.0834063298428));
#154396=CARTESIAN_POINT('Ctrl Pts',(-17.7502562818926,-21.4186339846309,
11.1194278825506));
#154397=CARTESIAN_POINT('Ctrl Pts',(-19.4306370706601,-21.8291474349523,
11.1978413708189));
#154398=CARTESIAN_POINT('Ctrl Pts',(-21.0857645353049,-20.4522478666649,
11.2922755722919));
#154399=CARTESIAN_POINT('Ctrl Pts',(-21.2926071426957,-19.2766421748681,
11.3506882210569));
#154400=CARTESIAN_POINT('Ctrl Pts',(-21.2907951752863,-18.9535971086061,
11.3667089342616));
#154401=CARTESIAN_POINT('Ctrl Pts',(-21.2939995125392,-18.9535798097909,
11.3667098902285));
#154402=CARTESIAN_POINT('Ctrl Pts',(-21.2940518853803,-18.8687123476393,
11.3709134538372));
#154403=CARTESIAN_POINT('Ctrl Pts',(-21.2898797137862,-18.7838299700766,
11.3751170174459));
#154404=CARTESIAN_POINT('Ctrl Pts',(-21.2815050782104,-18.699377996817,
11.3793205810546));
#154405=CARTESIAN_POINT('Ctrl Pts',(-21.2731292177987,-18.6149136719984,
11.3835247594572));
#154406=CARTESIAN_POINT('Ctrl Pts',(-21.2605497166712,-18.5308803238371,
11.3877289378599));
#154407=CARTESIAN_POINT('Ctrl Pts',(-21.2438404672875,-18.4477175109462,
11.3919331162626));
#154408=CARTESIAN_POINT('Ctrl Pts',(-21.2271240709727,-18.3645191274038,
11.3961390928892));
#154409=CARTESIAN_POINT('Ctrl Pts',(-21.2062745049673,-18.2821924593938,
11.4003450695159));
#154410=CARTESIAN_POINT('Ctrl Pts',(-21.1814163656274,-18.2011650425965,
11.4045510461425));
#154411=CARTESIAN_POINT('Ctrl Pts',(-21.1565238219894,-18.1200254817903,
11.408762843948));
#154412=CARTESIAN_POINT('Ctrl Pts',(-21.1276117659034,-18.0401891906194,
11.4129746417534));
#154413=CARTESIAN_POINT('Ctrl Pts',(-21.0948539828413,-17.9620664306619,
11.4171864395589));
#154414=CARTESIAN_POINT('Ctrl Pts',(-21.0620694457193,-17.8838798659899,
11.4214016772397));
#154415=CARTESIAN_POINT('Ctrl Pts',(-21.0254331231614,-17.8074100228063,
11.4256169149205));
#154416=CARTESIAN_POINT('Ctrl Pts',(-20.985165001354,-17.7330430127856,
11.4298321526013));
#154417=CARTESIAN_POINT('Ctrl Pts',(-20.9448260993907,-17.6585452862494,
11.4340547994973));
#154418=CARTESIAN_POINT('Ctrl Pts',(-20.9008428915851,-17.5861581518394,
11.4382774463933));
#154419=CARTESIAN_POINT('Ctrl Pts',(-20.853478708255,-17.5162388759777,
11.4425000932894));
#154420=CARTESIAN_POINT('Ctrl Pts',(-20.8410561777281,-17.497900666011,
11.4436075959693));
#154421=CARTESIAN_POINT('Ctrl Pts',(-20.828401284867,-17.4797320374709,
11.4447150986492));
#154422=CARTESIAN_POINT('Ctrl Pts',(-20.8155192213963,-17.4617390393097,
11.4458226013291));
#154423=CARTESIAN_POINT('Ctrl Pts',(-20.7668450946151,-17.3937535433782,
11.4500072357222));
#154424=CARTESIAN_POINT('Ctrl Pts',(-20.7147461245074,-17.3280286903786,
11.4541918701152));
#154425=CARTESIAN_POINT('Ctrl Pts',(-20.6594597008472,-17.2649300724589,
11.4583765045082));
#154426=CARTESIAN_POINT('Ctrl Pts',(-20.6042519705678,-17.2019212676116,
11.4625551825922));
#154427=CARTESIAN_POINT('Ctrl Pts',(-20.5458660991114,-17.1415316158067,
11.4667338606761));
#154428=CARTESIAN_POINT('Ctrl Pts',(-20.4845818988857,-17.0840966258144,
11.4709125387601));
#154429=CARTESIAN_POINT('Ctrl Pts',(-20.4221992234151,-17.0256321549044,
11.4751661166455));
#154430=CARTESIAN_POINT('Ctrl Pts',(-20.3568135727525,-16.9702297043269,
11.479419694531));
#154431=CARTESIAN_POINT('Ctrl Pts',(-20.2887620518452,-16.9182067553111,
11.4836732724164));
#154432=CARTESIAN_POINT('Ctrl Pts',(-20.2220298424622,-16.8671923726764,
11.4878443863944));
#154433=CARTESIAN_POINT('Ctrl Pts',(-20.1527345889107,-16.8194279167436,
11.4920155003723));
#154434=CARTESIAN_POINT('Ctrl Pts',(-20.0812289339446,-16.7751733648399,
11.4961866143503));
#154435=CARTESIAN_POINT('Ctrl Pts',(-20.0097472733917,-16.7309336629786,
11.5003563286706));
#154436=CARTESIAN_POINT('Ctrl Pts',(-19.9360570753459,-16.6902017679483,
11.504526042991));
#154437=CARTESIAN_POINT('Ctrl Pts',(-19.8605396057914,-16.6531941107211,
11.5086957573114));
#154438=CARTESIAN_POINT('Ctrl Pts',(-19.7850248234724,-16.6161877703851,
11.5128653232554));
#154439=CARTESIAN_POINT('Ctrl Pts',(-19.7076833123966,-16.582905606034,
11.5170348891995));
#154440=CARTESIAN_POINT('Ctrl Pts',(-19.6289193227213,-16.5535172700601,
11.5212044551435));
#154441=CARTESIAN_POINT('Ctrl Pts',(-19.5473860883349,-16.5230956764478,
11.5255206178824));
#154442=CARTESIAN_POINT('Ctrl Pts',(-19.4643289796725,-16.4968470041692,
11.5298367806213));
#154443=CARTESIAN_POINT('Ctrl Pts',(-19.3802151086559,-16.4749037093111,
11.5341529433603));
#154444=CARTESIAN_POINT('Ctrl Pts',(-19.2988412381404,-16.453675214975,
11.5383285075519));
#154445=CARTESIAN_POINT('Ctrl Pts',(-19.2164788667989,-16.436475960301,
11.5425040717436));
#154446=CARTESIAN_POINT('Ctrl Pts',(-19.1335609462705,-16.4233736831601,
11.5466796359353));
#154447=CARTESIAN_POINT('Ctrl Pts',(-19.046455038695,-16.4096096411485,
11.5510660979478));
#154448=CARTESIAN_POINT('Ctrl Pts',(-18.9587365661201,-16.4003673913993,
11.5554525599604));
#154449=CARTESIAN_POINT('Ctrl Pts',(-18.8709107816369,-16.3956636688668,
11.5598390219729));
#154450=CARTESIAN_POINT('Ctrl Pts',(-18.7830849971537,-16.3909599463343,
11.5642254839855));
#154451=CARTESIAN_POINT('Ctrl Pts',(-18.6951524811211,-16.3907946760441,
11.568611945998));
#154452=CARTESIAN_POINT('Ctrl Pts',(-18.607613246377,-16.3951217493771,
11.5729984080105));
#154453=CARTESIAN_POINT('Ctrl Pts',(-18.5241018215877,-16.3992497276517,
11.5771830424036));
#154454=CARTESIAN_POINT('Ctrl Pts',(-18.4406374370144,-16.4074811003133,
11.5813676767966));
#154455=CARTESIAN_POINT('Ctrl Pts',(-18.3576559923793,-16.4198141482253,
11.5855523111897));
#154456=CARTESIAN_POINT('Ctrl Pts',(-18.2747926615594,-16.4321296415702,
11.5897309892736));
#154457=CARTESIAN_POINT('Ctrl Pts',(-18.1924113564174,-16.4485351465589,
11.5939096673576));
#154458=CARTESIAN_POINT('Ctrl Pts',(-18.1109456438827,-16.4689769897717,
11.5980883454415));
#154459=CARTESIAN_POINT('Ctrl Pts',(-18.0280197169993,-16.4897852383328,
11.602341923327));
#154460=CARTESIAN_POINT('Ctrl Pts',(-17.9460430111247,-16.5147759273295,
11.6065955012124));
#154461=CARTESIAN_POINT('Ctrl Pts',(-17.8654649462447,-16.5438374514169,
11.6108490790978));
#154462=CARTESIAN_POINT('Ctrl Pts',(-17.7864490443875,-16.572335561151,
11.6150201930758));
#154463=CARTESIAN_POINT('Ctrl Pts',(-17.708778489378,-16.6047479091043,
11.6191913070537));
#154464=CARTESIAN_POINT('Ctrl Pts',(-17.6328627598405,-16.6409186993241,
11.6233624210317));
#154465=CARTESIAN_POINT('Ctrl Pts',(-17.5569725045593,-16.6770773520858,
11.6275321353521));
#154466=CARTESIAN_POINT('Ctrl Pts',(-17.4828363202439,-16.7169917446773,
11.6317018496724));
#154467=CARTESIAN_POINT('Ctrl Pts',(-17.4108425631367,-16.7604584427227,
11.6358715639928));
#154468=CARTESIAN_POINT('Ctrl Pts',(-17.3388513678763,-16.8039235940365,
11.6400411299369));
#154469=CARTESIAN_POINT('Ctrl Pts',(-17.2690028416262,-16.8509405609746,
11.6442106958809));
#154470=CARTESIAN_POINT('Ctrl Pts',(-17.2016584481431,-16.9012612627512,
11.648380261825));
#154471=CARTESIAN_POINT('Ctrl Pts',(-17.1319463088635,-16.9533511783249,
11.6526964245639));
#154472=CARTESIAN_POINT('Ctrl Pts',(-17.0649180918033,-17.0089811541786,
11.6570125873028));
#154473=CARTESIAN_POINT('Ctrl Pts',(-17.0009380103939,-17.0678301190757,
11.6613287500417));
#154474=CARTESIAN_POINT('Ctrl Pts',(-16.9390420734068,-17.1247620851311,
11.6655043142334));
#154475=CARTESIAN_POINT('Ctrl Pts',(-16.8799990325859,-17.1847061749561,
11.6696798784251));
#154476=CARTESIAN_POINT('Ctrl Pts',(-16.8241001932714,-17.2473350099629,
11.6738554426168));
#154477=CARTESIAN_POINT('Ctrl Pts',(-16.7653780364702,-17.31312707854,11.6782419046293));
#154478=CARTESIAN_POINT('Ctrl Pts',(-16.7101264215565,-17.3818817777301,
11.6826283666418));
#154479=CARTESIAN_POINT('Ctrl Pts',(-16.6586329038938,-17.4531833279551,
11.6870148286544));
#154480=CARTESIAN_POINT('Ctrl Pts',(-16.6071393862312,-17.52448487818,11.6914012906669));
#154481=CARTESIAN_POINT('Ctrl Pts',(-16.5594042169153,-17.5983327508676,
11.6957877526794));
#154482=CARTESIAN_POINT('Ctrl Pts',(-16.5156592733601,-17.6742815566288,
11.700174214692));
#154483=CARTESIAN_POINT('Ctrl Pts',(-16.4739270995034,-17.7467358452539,
11.704358849085));
#154484=CARTESIAN_POINT('Ctrl Pts',(-16.4356706929265,-17.8213716700561,
11.7085434834781));
#154485=CARTESIAN_POINT('Ctrl Pts',(-16.4011245523601,-17.8978215778158,
11.7127281178711));
#154486=CARTESIAN_POINT('Ctrl Pts',(-16.3666275839487,-17.9741626685945,
11.7169067959551));
#154487=CARTESIAN_POINT('Ctrl Pts',(-16.3358305794284,-18.0523122977899,
11.721085474039));
#154488=CARTESIAN_POINT('Ctrl Pts',(-16.308923089503,-18.1318768518237,
11.7252641521229));
#154489=CARTESIAN_POINT('Ctrl Pts',(-16.2815333021588,-18.2128675433067,
11.7295177300084));
#154490=CARTESIAN_POINT('Ctrl Pts',(-16.258174080664,-18.2953239658203,
11.7337713078938));
#154491=CARTESIAN_POINT('Ctrl Pts',(-16.2389948450999,-18.3788078184223,
11.7380248857792));
#154492=CARTESIAN_POINT('Ctrl Pts',(-16.2201874364424,-18.4606731736363,
11.7421959997572));
#154493=CARTESIAN_POINT('Ctrl Pts',(-16.2053994934178,-18.5435260079658,
11.7463671137352));
#154494=CARTESIAN_POINT('Ctrl Pts',(-16.194721659298,-18.6269376852947,
11.7505382277131));
#154495=CARTESIAN_POINT('Ctrl Pts',(-16.1840474082286,-18.7103213730297,
11.7547079420335));
#154496=CARTESIAN_POINT('Ctrl Pts',(-16.1774805853424,-18.7942630754067,
11.7588776563538));
#154497=CARTESIAN_POINT('Ctrl Pts',(-16.1750603443919,-18.8783261311156,
11.7630473706742));
#154498=CARTESIAN_POINT('Ctrl Pts',(-16.172640189564,-18.9623861955001,
11.7672169366182));
#154499=CARTESIAN_POINT('Ctrl Pts',(-16.1743663356855,-19.0465671447637,
11.7713865025623));
#154500=CARTESIAN_POINT('Ctrl Pts',(-16.1802258395509,-19.1304307636657,
11.7755560685063));
#154501=CARTESIAN_POINT('Ctrl Pts',(-16.1862913563437,-19.2172429239514,
11.7798722312452));
#154502=CARTESIAN_POINT('Ctrl Pts',(-16.1967862597981,-19.3037144978774,
11.7841883939842));
#154503=CARTESIAN_POINT('Ctrl Pts',(-16.2116377216372,-19.3893654498155,
11.7885045567231));
#154504=CARTESIAN_POINT('Ctrl Pts',(-16.2260053986689,-19.4722263310029,
11.7926801209148));
#154505=CARTESIAN_POINT('Ctrl Pts',(-16.2444500136973,-19.5543187834622,
11.7968556851065));
#154506=CARTESIAN_POINT('Ctrl Pts',(-16.2668539711945,-19.635220661682,
11.8010312492981));
#154507=CARTESIAN_POINT('Ctrl Pts',(-16.2903894993245,-19.7202087014447,
11.8054177113107));
#154508=CARTESIAN_POINT('Ctrl Pts',(-16.3182946694534,-19.8038821804653,
11.8098041733232));
#154509=CARTESIAN_POINT('Ctrl Pts',(-16.3503755250187,-19.8857742565899,
11.8141906353358));
#154510=CARTESIAN_POINT('Ctrl Pts',(-16.382456380584,-19.9676663327144,
11.8185770973483));
#154511=CARTESIAN_POINT('Ctrl Pts',(-16.4187126130535,-20.047776508705,
11.8229635593609));
#154512=CARTESIAN_POINT('Ctrl Pts',(-16.4588952312817,-20.1256687315232,
11.8273500213734));
#154513=CARTESIAN_POINT('Ctrl Pts',(-16.4972321909917,-20.1999832271826,
11.8315350054501));
#154514=CARTESIAN_POINT('Ctrl Pts',(-16.5392854659906,-20.2725556853913,
11.8357199895268));
#154515=CARTESIAN_POINT('Ctrl Pts',(-16.5848729683257,-20.3429899358826,
11.8399049736034));
#154516=CARTESIAN_POINT('Ctrl Pts',(-16.6303841734451,-20.4133063045659,
11.8440829535097));
#154517=CARTESIAN_POINT('Ctrl Pts',(-16.6794175976995,-20.4814911976367,
11.8482609334161));
#154518=CARTESIAN_POINT('Ctrl Pts',(-16.7317449889769,-20.5471723639885,
11.8524389133224));
#154519=CARTESIAN_POINT('Ctrl Pts',(-16.7840217296592,-20.612789953883,
11.8566128491293));
#154520=CARTESIAN_POINT('Ctrl Pts',(-16.8395858226484,-20.6759082705201,
11.8607867849363));
#154521=CARTESIAN_POINT('Ctrl Pts',(-16.8981658620059,-20.7361841322508,
11.8649607207433));
#154522=CARTESIAN_POINT('Ctrl Pts',(-16.9567039826349,-20.7964168617556,
11.8691316697636));
#154523=CARTESIAN_POINT('Ctrl Pts',(-17.0182534419654,-20.8538108487294,
11.8733026187839));
#154524=CARTESIAN_POINT('Ctrl Pts',(-17.0825036449483,-20.9080572050048,
11.8774735678041));
#154525=CARTESIAN_POINT('Ctrl Pts',(-17.1125774867215,-20.9334485074389,
11.8794258800935));
#154526=CARTESIAN_POINT('Ctrl Pts',(-17.1432425028621,-20.9581506972719,
11.8813781923829));
#154527=CARTESIAN_POINT('Ctrl Pts',(-17.1744641402401,-20.9821349467765,
11.8833305046723));
#154528=CARTESIAN_POINT('Origin',(-18.734,-18.952,-1.76670989022851));
#154529=CARTESIAN_POINT('',(-17.1744641402401,-20.9821349467765,12.7499597538068));
#154530=CARTESIAN_POINT('',(-17.1750494479187,-20.9813915763786,12.6831923855689));
#154531=CARTESIAN_POINT('',(-17.1744641402401,-20.9821349467765,-1.76670989022851));
#154532=CARTESIAN_POINT('',(-21.2939989766127,-18.9542890482673,12.2332901098107));
#154533=CARTESIAN_POINT('Ctrl Pts',(-21.2939989766127,-18.9542890482673,
12.2332901098107));
#154534=CARTESIAN_POINT('Ctrl Pts',(-21.2940747905549,-18.869501140071,
12.2375129674107));
#154535=CARTESIAN_POINT('Ctrl Pts',(-21.2899336304853,-18.7845778436852,
12.2417358250107));
#154536=CARTESIAN_POINT('Ctrl Pts',(-21.2815646644669,-18.699979603286,
12.2459586826108));
#154537=CARTESIAN_POINT('Ctrl Pts',(-21.2734134565488,-18.6175825848873,
12.2500716626647));
#154538=CARTESIAN_POINT('Ctrl Pts',(-21.2612518149667,-18.5354944186517,
12.2541846427187));
#154539=CARTESIAN_POINT('Ctrl Pts',(-21.2451224198776,-18.4541403888767,
12.2582976227727));
#154540=CARTESIAN_POINT('Ctrl Pts',(-21.2290007459443,-18.3728253033476,
12.2624086339395));
#154541=CARTESIAN_POINT('Ctrl Pts',(-21.2089151790601,-18.2922441216167,
12.2665196451063));
#154542=CARTESIAN_POINT('Ctrl Pts',(-21.1849598944702,-18.2128142346483,
12.2706306562731));
#154543=CARTESIAN_POINT('Ctrl Pts',(-21.1610084101084,-18.1333969483105,
12.2747410152756));
#154544=CARTESIAN_POINT('Ctrl Pts',(-21.133188564531,-18.0551310480641,
12.2788513742782));
#154545=CARTESIAN_POINT('Ctrl Pts',(-21.1016446063283,-17.9784194855459,
12.2829617332807));
#154546=CARTESIAN_POINT('Ctrl Pts',(-21.0685960771622,-17.8980489659376,
12.2872681465249));
#154547=CARTESIAN_POINT('Ctrl Pts',(-21.031459503672,-17.8193852938559,
12.2915745597691));
#154548=CARTESIAN_POINT('Ctrl Pts',(-20.9904568914618,-17.7428671301405,
12.2958809730133));
#154549=CARTESIAN_POINT('Ctrl Pts',(-20.9512718262792,-17.669740832297,
12.2999964933321));
#154550=CARTESIAN_POINT('Ctrl Pts',(-20.9085564982552,-17.5985742591841,
12.304112013651));
#154551=CARTESIAN_POINT('Ctrl Pts',(-20.8625501361326,-17.5297221375659,
12.3082275339698));
#154552=CARTESIAN_POINT('Ctrl Pts',(-20.8165130556118,-17.4608240434608,
12.3123458022171));
#154553=CARTESIAN_POINT('Ctrl Pts',(-20.7671808550883,-17.3942438526559,
12.3164640704644));
#154554=CARTESIAN_POINT('Ctrl Pts',(-20.7148334041519,-17.3303036582036,
12.3205823387118));
#154555=CARTESIAN_POINT('Ctrl Pts',(-20.6624054653519,-17.2662651512345,
12.3247069390843));
#154556=CARTESIAN_POINT('Ctrl Pts',(-20.6069533520103,-17.204875081262,
12.3288315394568));
#154557=CARTESIAN_POINT('Ctrl Pts',(-20.5487934990227,-17.146418499235,
12.3329561398293));
#154558=CARTESIAN_POINT('Ctrl Pts',(-20.5408850965653,-17.1384697484523,
12.3335169906232));
#154559=CARTESIAN_POINT('Ctrl Pts',(-20.5329266770602,-17.1305751748486,
12.3340778414171));
#154560=CARTESIAN_POINT('Ctrl Pts',(-20.524919080494,-17.1227354354489,
12.334638692211));
#154561=CARTESIAN_POINT('Ctrl Pts',(-20.4651725946905,-17.0642413698601,
12.338823326604));
#154562=CARTESIAN_POINT('Ctrl Pts',(-20.4024461555816,-17.0085686402269,
12.3430079609971));
#154563=CARTESIAN_POINT('Ctrl Pts',(-20.3370370650427,-16.9560360303604,
12.3471925953901));
#154564=CARTESIAN_POINT('Ctrl Pts',(-20.2717210762481,-16.9035781941618,
12.3513712734741));
#154565=CARTESIAN_POINT('Ctrl Pts',(-20.2037303762193,-16.8542518853563,
12.355549951558));
#154566=CARTESIAN_POINT('Ctrl Pts',(-20.1333988170804,-16.8083388908799,
12.3597286296419));
#154567=CARTESIAN_POINT('Ctrl Pts',(-20.0618066152903,-16.7616029389746,
12.3639822075274));
#154568=CARTESIAN_POINT('Ctrl Pts',(-19.9877891536757,-16.7184042096101,
12.3682357854128));
#154569=CARTESIAN_POINT('Ctrl Pts',(-19.9117335730786,-16.6789967816029,
12.3724893632982));
#154570=CARTESIAN_POINT('Ctrl Pts',(-19.8371524783216,-16.6403533434849,
12.3766604772762));
#154571=CARTESIAN_POINT('Ctrl Pts',(-19.760612012467,-16.605355736394,12.3808315912541));
#154572=CARTESIAN_POINT('Ctrl Pts',(-19.6825046263014,-16.5741987101768,
12.3850027052321));
#154573=CARTESIAN_POINT('Ctrl Pts',(-19.6044234498237,-16.5430521390007,
12.3891724195525));
#154574=CARTESIAN_POINT('Ctrl Pts',(-19.5247768242089,-16.5157437595369,
12.3933421338728));
#154575=CARTESIAN_POINT('Ctrl Pts',(-19.443977821747,-16.4924204642607,
12.3975118481932));
#154576=CARTESIAN_POINT('Ctrl Pts',(-19.3631816944604,-16.4690979989275,
12.4016814141372));
#154577=CARTESIAN_POINT('Ctrl Pts',(-19.281233714082,-16.449760462599,12.4058509800813));
#154578=CARTESIAN_POINT('Ctrl Pts',(-19.1985614595122,-16.4345046871273,
12.4100205460253));
#154579=CARTESIAN_POINT('Ctrl Pts',(-19.112982550459,-16.4187125374101,
12.4143367087642));
#154580=CARTESIAN_POINT('Ctrl Pts',(-19.0266280073015,-16.4072946141391,
12.4186528715032));
#154581=CARTESIAN_POINT('Ctrl Pts',(-18.9399808515254,-16.400300196182,
12.4229690342421));
#154582=CARTESIAN_POINT('Ctrl Pts',(-18.8561562177351,-16.3935336206541,
12.4271445984338));
#154583=CARTESIAN_POINT('Ctrl Pts',(-18.7720582145669,-16.3909067522804,
12.4313201626255));
#154584=CARTESIAN_POINT('Ctrl Pts',(-18.6881249777989,-16.3924110716097,
12.4354957268171));
#154585=CARTESIAN_POINT('Ctrl Pts',(-18.5999524727738,-16.3939913705322,
12.4398821888297));
#154586=CARTESIAN_POINT('Ctrl Pts',(-18.5119623987477,-16.4001311167978,
12.4442686508422));
#154587=CARTESIAN_POINT('Ctrl Pts',(-18.4246552312346,-16.4107590011891,
12.4486551128548));
#154588=CARTESIAN_POINT('Ctrl Pts',(-18.3373480637215,-16.4213868855804,
12.4530415748673));
#154589=CARTESIAN_POINT('Ctrl Pts',(-18.2507243612257,-16.4365027334242,
12.4574280368799));
#154590=CARTESIAN_POINT('Ctrl Pts',(-18.1652685194104,-16.4559742583486,
12.4618144988924));
#154591=CARTESIAN_POINT('Ctrl Pts',(-18.083744627553,-16.4745498695476,
12.4659991332854));
#154592=CARTESIAN_POINT('Ctrl Pts',(-18.0029800405432,-16.4971582855303,
12.4701837676785));
#154593=CARTESIAN_POINT('Ctrl Pts',(-17.923403728984,-16.5237220740997,
12.4743684020715));
#154594=CARTESIAN_POINT('Ctrl Pts',(-17.8439406844548,-16.5502480524038,
12.4785470801555));
#154595=CARTESIAN_POINT('Ctrl Pts',(-17.7656629884269,-16.5807180759576,
12.4827257582394));
#154596=CARTESIAN_POINT('Ctrl Pts',(-17.6889882869429,-16.6150039538815,
12.4869044363234));
#154597=CARTESIAN_POINT('Ctrl Pts',(-17.6109392465397,-16.6499043815265,
12.4911580142088));
#154598=CARTESIAN_POINT('Ctrl Pts',(-17.5345517033716,-16.6887587003509,
12.4954115920942));
#154599=CARTESIAN_POINT('Ctrl Pts',(-17.4602488495092,-16.7313789142172,
12.4996651699797));
#154600=CARTESIAN_POINT('Ctrl Pts',(-17.3873865014589,-16.7731728520712,
12.5038362839576));
#154601=CARTESIAN_POINT('Ctrl Pts',(-17.3165291499245,-16.8185877301275,
12.5080073979356));
#154602=CARTESIAN_POINT('Ctrl Pts',(-17.2480529748744,-16.8673989737793,
12.5121785119135));
#154603=CARTESIAN_POINT('Ctrl Pts',(-17.1795997776662,-16.9161938383469,
12.5163482262339));
#154604=CARTESIAN_POINT('Ctrl Pts',(-17.1135265443543,-16.9683825382779,
12.5205179405543));
#154605=CARTESIAN_POINT('Ctrl Pts',(-17.0501803764602,-17.0236972552573,
12.5246876548747));
#154606=CARTESIAN_POINT('Ctrl Pts',(-16.9868364626947,-17.0790100039016,
12.5288572208187));
#154607=CARTESIAN_POINT('Ctrl Pts',(-16.9262197673615,-17.1374482452015,
12.5330267867627));
#154608=CARTESIAN_POINT('Ctrl Pts',(-16.8686431510734,-17.1987048662126,
12.5371963527068));
#154609=CARTESIAN_POINT('Ctrl Pts',(-16.809042211985,-17.2621151944502,
12.5415125154457));
#154610=CARTESIAN_POINT('Ctrl Pts',(-16.752699469072,-17.3285453940344,
12.5458286781846));
#154611=CARTESIAN_POINT('Ctrl Pts',(-16.6999178084324,-17.3976159940518,
12.5501448409235));
#154612=CARTESIAN_POINT('Ctrl Pts',(-16.6488555048365,-17.4644366265386,
12.5543204051152));
#154613=CARTESIAN_POINT('Ctrl Pts',(-16.6011260701749,-17.5337278643774,
12.5584959693069));
#154614=CARTESIAN_POINT('Ctrl Pts',(-16.5569594955243,-17.6051166932981,
12.5626715334986));
#154615=CARTESIAN_POINT('Ctrl Pts',(-16.5105621721843,-17.6801112022566,
12.5670579955111));
#154616=CARTESIAN_POINT('Ctrl Pts',(-16.4680973689511,-17.7574202579854,
12.5714444575237));
#154617=CARTESIAN_POINT('Ctrl Pts',(-16.4297760239617,-17.8365844414523,
12.5758309195362));
#154618=CARTESIAN_POINT('Ctrl Pts',(-16.3914546789723,-17.9157486249192,
12.5802173815487));
#154619=CARTESIAN_POINT('Ctrl Pts',(-16.3572769476616,-17.9967673719631,
12.5846038435613));
#154620=CARTESIAN_POINT('Ctrl Pts',(-16.3273937923111,-18.0791617783844,
12.5889903055738));
#154621=CARTESIAN_POINT('Ctrl Pts',(-16.2988856052357,-18.1577650960284,
12.5931749399669));
#154622=CARTESIAN_POINT('Ctrl Pts',(-16.274179366091,-18.2379128391994,
12.5973595743599));
#154623=CARTESIAN_POINT('Ctrl Pts',(-16.2534421603043,-18.3192023989268,
12.601544208753));
#154624=CARTESIAN_POINT('Ctrl Pts',(-16.2327344713631,-18.4003762530276,
12.6057228868369));
#154625=CARTESIAN_POINT('Ctrl Pts',(-16.2159847069801,-18.4826882535132,
12.6099015649209));
#154626=CARTESIAN_POINT('Ctrl Pts',(-16.2033111427937,-18.565717838864,
12.6140802430048));
#154627=CARTESIAN_POINT('Ctrl Pts',(-16.1904104140776,-18.6502356698599,
12.6183338208902));
#154628=CARTESIAN_POINT('Ctrl Pts',(-16.1817336190671,-18.7354966109228,
12.6225873987757));
#154629=CARTESIAN_POINT('Ctrl Pts',(-16.177351748603,-18.821043065749,12.6268409766611));
#154630=CARTESIAN_POINT('Ctrl Pts',(-16.1730548292482,-18.9049310356184,
12.6310120906391));
#154631=CARTESIAN_POINT('Ctrl Pts',(-16.1728878141637,-18.9890930669704,
12.635183204617));
#154632=CARTESIAN_POINT('Ctrl Pts',(-16.1768654907269,-19.0730912940081,
12.639354318595));
#154633=CARTESIAN_POINT('Ctrl Pts',(-16.1808418325423,-19.1570613346296,
12.6435240329154));
#154634=CARTESIAN_POINT('Ctrl Pts',(-16.1889600821297,-19.2408672209648,
12.6476937472357));
#154635=CARTESIAN_POINT('Ctrl Pts',(-16.2011829261397,-19.3240721305897,
12.6518634615561));
#154636=CARTESIAN_POINT('Ctrl Pts',(-16.2134053352084,-19.4072740794267,
12.6560330275002));
#154637=CARTESIAN_POINT('Ctrl Pts',(-16.2297319805921,-19.4898746390488,
12.6602025934442));
#154638=CARTESIAN_POINT('Ctrl Pts',(-16.2500739744222,-19.5714445087795,
12.6643721593882));
#154639=CARTESIAN_POINT('Ctrl Pts',(-16.2711311676607,-19.6558822745028,
12.6686883221272));
#154640=CARTESIAN_POINT('Ctrl Pts',(-16.2964911945898,-19.7392150119469,
12.6730044848661));
#154641=CARTESIAN_POINT('Ctrl Pts',(-16.3259989267242,-19.8209826414278,
12.677320647605));
#154642=CARTESIAN_POINT('Ctrl Pts',(-16.354545447588,-19.9000866989788,
12.6814962117967));
#154643=CARTESIAN_POINT('Ctrl Pts',(-16.3869733753123,-19.9777256330122,
12.6856717759884));
#154644=CARTESIAN_POINT('Ctrl Pts',(-16.4230935537345,-20.0535041518799,
12.6898473401801));
#154645=CARTESIAN_POINT('Ctrl Pts',(-16.4610380765012,-20.1331100635892,
12.6942338021926));
#154646=CARTESIAN_POINT('Ctrl Pts',(-16.5030573653645,-20.2106621684913,
12.6986202642052));
#154647=CARTESIAN_POINT('Ctrl Pts',(-16.5488792984355,-20.2857344261862,
12.7030067262177));
#154648=CARTESIAN_POINT('Ctrl Pts',(-16.5947012315065,-20.3608066838811,
12.7073931882302));
#154649=CARTESIAN_POINT('Ctrl Pts',(-16.6443254185492,-20.433398658303,
12.7117796502428));
#154650=CARTESIAN_POINT('Ctrl Pts',(-16.6974308899397,-20.5031241923032,
12.7161661122553));
#154651=CARTESIAN_POINT('Ctrl Pts',(-16.7480908287789,-20.5696388318591,
12.7203505755782));
#154652=CARTESIAN_POINT('Ctrl Pts',(-16.8021070326506,-20.6337927963332,
12.724535038901));
#154653=CARTESIAN_POINT('Ctrl Pts',(-16.8592314426267,-20.6952277121147,
12.7287195022239));
#154654=CARTESIAN_POINT('Ctrl Pts',(-16.9162677654097,-20.756567893801,
12.7328975130051));
#154655=CARTESIAN_POINT('Ctrl Pts',(-16.9764024588243,-20.8151970253541,
12.7370755237864));
#154656=CARTESIAN_POINT('Ctrl Pts',(-17.0393460611412,-20.8707881663984,
12.7412535345677));
#154657=CARTESIAN_POINT('Ctrl Pts',(-17.0830670909289,-20.9094021294393,
12.7441556076474));
#154658=CARTESIAN_POINT('Ctrl Pts',(-17.1281424629339,-20.94655094929,12.7470576807271));
#154659=CARTESIAN_POINT('Ctrl Pts',(-17.1744641402401,-20.9821349467765,
12.7499597538068));
#154660=CARTESIAN_POINT('Ctrl Pts',(-17.1744641402401,-20.9821349467765,
11.949868723648));
#154661=CARTESIAN_POINT('Ctrl Pts',(-17.1916066249818,-20.995303686974,
11.9509495731542));
#154662=CARTESIAN_POINT('Ctrl Pts',(-17.2089081277772,-21.0082493016174,
11.9520304226604));
#154663=CARTESIAN_POINT('Ctrl Pts',(-17.2263622218881,-21.0209679383717,
11.9531112721667));
#154664=CARTESIAN_POINT('Ctrl Pts',(-17.2939377743551,-21.0702096177068,
11.9572959065597));
#154665=CARTESIAN_POINT('Ctrl Pts',(-17.3640540780906,-21.1162287760929,
11.9614805409527));
#154666=CARTESIAN_POINT('Ctrl Pts',(-17.4363708665884,-21.1587529612807,
11.9656651753458));
#154667=CARTESIAN_POINT('Ctrl Pts',(-17.5085847210887,-21.2012166185545,
11.9698438534297));
#154668=CARTESIAN_POINT('Ctrl Pts',(-17.5829924458174,-21.2401949526837,
11.9740225315137));
#154669=CARTESIAN_POINT('Ctrl Pts',(-17.659222956839,-21.2754574038476,
11.9782012095976));
#154670=CARTESIAN_POINT('Ctrl Pts',(-17.7368198449848,-21.3113519091059,
11.9824547874831));
#154671=CARTESIAN_POINT('Ctrl Pts',(-17.8163051194007,-21.3433957227619,
11.9867083653685));
#154672=CARTESIAN_POINT('Ctrl Pts',(-17.8972589731891,-21.3713934062181,
11.9909619432539));
#154673=CARTESIAN_POINT('Ctrl Pts',(-17.9766433785533,-21.3988482999474,
11.9951330572319));
#154674=CARTESIAN_POINT('Ctrl Pts',(-18.0574394740936,-21.4224123904404,
11.9993041712098));
#154675=CARTESIAN_POINT('Ctrl Pts',(-18.1392307762324,-21.4419497124358,
12.0034752851878));
#154676=CARTESIAN_POINT('Ctrl Pts',(-18.2209946325099,-21.461480478494,
12.0076449995081));
#154677=CARTESIAN_POINT('Ctrl Pts',(-18.303752585081,-21.4769870528098,
12.0118147138285));
#154678=CARTESIAN_POINT('Ctrl Pts',(-18.3870746644898,-21.4883838060477,
12.0159844281489));
#154679=CARTESIAN_POINT('Ctrl Pts',(-18.4703937789414,-21.4997801537403,
12.0201539940929));
#154680=CARTESIAN_POINT('Ctrl Pts',(-18.5542765244138,-21.5070669096296,
12.024323560037));
#154681=CARTESIAN_POINT('Ctrl Pts',(-18.6382858147563,-21.5102100763509,
12.028493125981));
#154682=CARTESIAN_POINT('Ctrl Pts',(-18.7252487681107,-21.5134637529366,
12.0328092887199));
#154683=CARTESIAN_POINT('Ctrl Pts',(-18.8123468034828,-21.5122770220956,
12.0371254514589));
#154684=CARTESIAN_POINT('Ctrl Pts',(-18.8990948495902,-21.5066709554537,
12.0414416141978));
#154685=CARTESIAN_POINT('Ctrl Pts',(-18.9830170872199,-21.501247505843,
12.0456171783895));
#154686=CARTESIAN_POINT('Ctrl Pts',(-19.0666113245951,-21.4916883190585,
12.0497927425811));
#154687=CARTESIAN_POINT('Ctrl Pts',(-19.1494452607497,-21.4780651684627,
12.0539683067728));
#154688=CARTESIAN_POINT('Ctrl Pts',(-19.2364629421006,-21.4637539449163,
12.0583547687854));
#154689=CARTESIAN_POINT('Ctrl Pts',(-19.3226409276417,-21.444957551129,
12.0627412307979));
#154690=CARTESIAN_POINT('Ctrl Pts',(-19.4074943094419,-21.4218189033104,
12.0671276928105));
#154691=CARTESIAN_POINT('Ctrl Pts',(-19.4923476912421,-21.3986802554918,
12.071514154823));
#154692=CARTESIAN_POINT('Ctrl Pts',(-19.5758759419182,-21.371199607226,
12.0759006168356));
#154693=CARTESIAN_POINT('Ctrl Pts',(-19.6576188802164,-21.3395778865008,
12.0802870788481));
#154694=CARTESIAN_POINT('Ctrl Pts',(-19.7356007047513,-21.3094111280209,
12.0844717132412));
#154695=CARTESIAN_POINT('Ctrl Pts',(-19.8122481596154,-21.2753637103369,
12.0886563476342));
#154696=CARTESIAN_POINT('Ctrl Pts',(-19.8871479757777,-21.2375742704974,
12.0928409820272));
#154697=CARTESIAN_POINT('Ctrl Pts',(-19.9619411813225,-21.1998386192481,
12.0970196601112));
#154698=CARTESIAN_POINT('Ctrl Pts',(-20.0349912820117,-21.1583717310105,
12.1011983381951));
#154699=CARTESIAN_POINT('Ctrl Pts',(-20.1059035528267,-21.1133608309908,
12.1053770162791));
#154700=CARTESIAN_POINT('Ctrl Pts',(-20.1780868751323,-21.0675431429372,
12.1096305941645));
#154701=CARTESIAN_POINT('Ctrl Pts',(-20.2480545228573,-21.0180533145438,
12.11388417205));
#154702=CARTESIAN_POINT('Ctrl Pts',(-20.3154149295588,-20.9651385497696,
12.1181377499354));
#154703=CARTESIAN_POINT('Ctrl Pts',(-20.3814694233334,-20.9132496409652,
12.1223088639134));
#154704=CARTESIAN_POINT('Ctrl Pts',(-20.4450164884367,-20.8580677061306,
12.1264799778913));
#154705=CARTESIAN_POINT('Ctrl Pts',(-20.5057163649395,-20.7998693466275,
12.1306510918693));
#154706=CARTESIAN_POINT('Ctrl Pts',(-20.5663958730126,-20.7416905161459,
12.1348208061896));
#154707=CARTESIAN_POINT('Ctrl Pts',(-20.6242297581416,-20.6804975893352,
12.13899052051));
#154708=CARTESIAN_POINT('Ctrl Pts',(-20.6789132852951,-20.6166057529285,
12.1431602348304));
#154709=CARTESIAN_POINT('Ctrl Pts',(-20.7335948665741,-20.5527161900675,
12.1473298007744));
#154710=CARTESIAN_POINT('Ctrl Pts',(-20.785126014285,-20.486128258616,12.1514993667185));
#154711=CARTESIAN_POINT('Ctrl Pts',(-20.8332415555809,-20.4171910767277,
12.1556689326625));
#154712=CARTESIAN_POINT('Ctrl Pts',(-20.8830487799517,-20.3458301485675,
12.1599850954014));
#154713=CARTESIAN_POINT('Ctrl Pts',(-20.9291954417206,-20.2719521294864,
12.1643012581404));
#154714=CARTESIAN_POINT('Ctrl Pts',(-20.9714366989051,-20.1959762933403,
12.1686174208793));
#154715=CARTESIAN_POINT('Ctrl Pts',(-21.0123019515798,-20.1224753620654,
12.172792985071));
#154716=CARTESIAN_POINT('Ctrl Pts',(-21.0495121634692,-20.0470116310055,
12.1769685492626));
#154717=CARTESIAN_POINT('Ctrl Pts',(-21.0828936882991,-19.96998744642,12.1811441134543));
#154718=CARTESIAN_POINT('Ctrl Pts',(-21.117961234591,-19.8890729533789,
12.1855305754669));
#154719=CARTESIAN_POINT('Ctrl Pts',(-21.1488029510882,-19.8064367740456,
12.1899170374794));
#154720=CARTESIAN_POINT('Ctrl Pts',(-21.1752765362399,-19.7225639970856,
12.1943034994919));
#154721=CARTESIAN_POINT('Ctrl Pts',(-21.2017501213916,-19.6386912201256,
12.1986899615045));
#154722=CARTESIAN_POINT('Ctrl Pts',(-21.2238555029593,-19.5535824262448,
12.203076423517));
#154723=CARTESIAN_POINT('Ctrl Pts',(-21.2415125421985,-19.4677333135615,
12.2074628855296));
#154724=CARTESIAN_POINT('Ctrl Pts',(-21.2654843862316,-19.3511814097151,
12.2134181072288));
#154725=CARTESIAN_POINT('Ctrl Pts',(-21.2813366135095,-19.2329068373031,
12.219373328928));
#154726=CARTESIAN_POINT('Ctrl Pts',(-21.2888788650992,-19.1138455580776,
12.2253285506272));
#154727=CARTESIAN_POINT('Ctrl Pts',(-21.2922399536332,-19.060787728371,
12.2279824036753));
#154728=CARTESIAN_POINT('Ctrl Pts',(-21.2939513313562,-19.0075739736056,
12.2306362567234));
#154729=CARTESIAN_POINT('Ctrl Pts',(-21.293998976612,-18.9542890490546,
12.2332901097715));
#154730=CARTESIAN_POINT('',(-21.2939992159918,-18.9499964727371,12.1667098902285));
#154731=CARTESIAN_POINT('Ctrl Pts',(-17.1744641402401,-20.9821349467765,
11.8833305046723));
#154732=CARTESIAN_POINT('Ctrl Pts',(-17.2411432256658,-21.0333573667355,
11.887499997654));
#154733=CARTESIAN_POINT('Ctrl Pts',(-17.3103630271814,-21.0813023994611,
11.8916694906356));
#154734=CARTESIAN_POINT('Ctrl Pts',(-17.3817636652371,-21.1257195989702,
11.8958389836172));
#154735=CARTESIAN_POINT('Ctrl Pts',(-17.4531713785687,-21.1701411998956,
11.9000088897648));
#154736=CARTESIAN_POINT('Ctrl Pts',(-17.5267599662335,-21.2110340315857,
11.9041787959124));
#154737=CARTESIAN_POINT('Ctrl Pts',(-17.6021424969676,-21.2481921942271,
11.90834870206));
#154738=CARTESIAN_POINT('Ctrl Pts',(-17.6776049649932,-21.2853897602004,
11.9125230300676));
#154739=CARTESIAN_POINT('Ctrl Pts',(-17.7548647608072,-21.3188445462589,
11.9166973580753));
#154740=CARTESIAN_POINT('Ctrl Pts',(-17.8335128509122,-21.3483978998338,
11.9208716860829));
#154741=CARTESIAN_POINT('Ctrl Pts',(-17.9122051113765,-21.3779678511702,
11.9250483584777));
#154742=CARTESIAN_POINT('Ctrl Pts',(-17.9922867803495,-21.4036318669961,
11.9292250308725));
#154743=CARTESIAN_POINT('Ctrl Pts',(-18.0733337771331,-21.425281250073,
11.9334017032672));
#154744=CARTESIAN_POINT('Ctrl Pts',(-18.1545198069368,-21.4469677718377,
11.9375855405836));
#154745=CARTESIAN_POINT('Ctrl Pts',(-18.2366740216876,-21.4646258106057,
11.9417693778999));
#154746=CARTESIAN_POINT('Ctrl Pts',(-18.3193625425945,-21.4781978898963,
11.9459532152163));
#154747=CARTESIAN_POINT('Ctrl Pts',(-18.3758383423869,-21.4874675445518,
11.9488107528291));
#154748=CARTESIAN_POINT('Ctrl Pts',(-18.4325632297361,-21.4948322585704,
11.951668290442));
#154749=CARTESIAN_POINT('Ctrl Pts',(-18.489398605575,-21.500287691342,11.9545258280548));
#154750=CARTESIAN_POINT('Ctrl Pts',(-18.5726294499945,-21.5082767346017,
11.9587104624479));
#154751=CARTESIAN_POINT('Ctrl Pts',(-18.6564069960724,-21.5121986934545,
11.9628950968409));
#154752=CARTESIAN_POINT('Ctrl Pts',(-18.7402996751639,-21.5119922488345,
11.967079731234));
#154753=CARTESIAN_POINT('Ctrl Pts',(-18.8240729434107,-21.5117860980629,
11.9712584093179));
#154754=CARTESIAN_POINT('Ctrl Pts',(-18.9079605630616,-21.507463217065,
11.9754370874019));
#154755=CARTESIAN_POINT('Ctrl Pts',(-18.9915257624727,-21.4990140324825,
11.9796157654858));
#154756=CARTESIAN_POINT('Ctrl Pts',(-19.0765888080259,-21.4904134023388,
11.9838693433713));
#154757=CARTESIAN_POINT('Ctrl Pts',(-19.1613172809487,-21.4775370395472,
11.9881229212567));
#154758=CARTESIAN_POINT('Ctrl Pts',(-19.2452503475953,-21.4604304020809,
11.9923764991421));
#154759=CARTESIAN_POINT('Ctrl Pts',(-19.327556207963,-21.4436554101627,
11.9965476131201));
#154760=CARTESIAN_POINT('Ctrl Pts',(-19.4090967563153,-21.4228128002074,
12.000718727098));
#154761=CARTESIAN_POINT('Ctrl Pts',(-19.4894442918872,-21.3979975310403,
12.004889841076));
#154762=CARTESIAN_POINT('Ctrl Pts',(-19.5697648660674,-21.3731905888764,
12.0090595553964));
#154763=CARTESIAN_POINT('Ctrl Pts',(-19.6488927833423,-21.3444137706278,
12.0132292697167));
#154764=CARTESIAN_POINT('Ctrl Pts',(-19.7264143560961,-21.3118122268126,
12.0173989840371));
#154765=CARTESIAN_POINT('Ctrl Pts',(-19.8039331702998,-21.2792118431002,
12.0215685499811));
#154766=CARTESIAN_POINT('Ctrl Pts',(-19.8798453299036,-21.2427871835461,
12.0257381159252));
#154767=CARTESIAN_POINT('Ctrl Pts',(-19.9537573024932,-21.2027314639944,
12.0299076818692));
#154768=CARTESIAN_POINT('Ctrl Pts',(-20.0302679288589,-21.1612674347574,
12.0342238446082));
#154769=CARTESIAN_POINT('Ctrl Pts',(-20.1046346343672,-21.1159125099134,
12.0385400073471));
#154770=CARTESIAN_POINT('Ctrl Pts',(-20.1764506132335,-21.0669317313763,
12.042856170086));
#154771=CARTESIAN_POINT('Ctrl Pts',(-20.245927194142,-21.0195464965481,
12.0470317342777));
#154772=CARTESIAN_POINT('Ctrl Pts',(-20.3130163291631,-20.9687683266671,
12.0512072984694));
#154773=CARTESIAN_POINT('Ctrl Pts',(-20.3773824427363,-20.9148790454091,
12.055382862661));
#154774=CARTESIAN_POINT('Ctrl Pts',(-20.4449995356902,-20.8582679446644,
12.0597693246736));
#154775=CARTESIAN_POINT('Ctrl Pts',(-20.509610870638,-20.7982235859987,
12.0641557866861));
#154776=CARTESIAN_POINT('Ctrl Pts',(-20.5708718020378,-20.7351158074781,
12.0685422486987));
#154777=CARTESIAN_POINT('Ctrl Pts',(-20.6321327334377,-20.6720080289575,
12.0729287107112));
#154778=CARTESIAN_POINT('Ctrl Pts',(-20.6900429364135,-20.6058373172988,
12.0773151727238));
#154779=CARTESIAN_POINT('Ctrl Pts',(-20.7443085775788,-20.5370108589259,
12.0817016347363));
#154780=CARTESIAN_POINT('Ctrl Pts',(-20.796026764239,-20.4714154002739,
12.0858821780095));
#154781=CARTESIAN_POINT('Ctrl Pts',(-20.8446312405901,-20.4031588919979,
12.0900627212828));
#154782=CARTESIAN_POINT('Ctrl Pts',(-20.8898359348525,-20.3325692383937,
12.0942432645561));
#154783=CARTESIAN_POINT('Ctrl Pts',(-20.9349778718437,-20.2620775837717,
12.0984180040186));
#154784=CARTESIAN_POINT('Ctrl Pts',(-20.9767291512524,-20.1892595981083,
12.1025927434812));
#154785=CARTESIAN_POINT('Ctrl Pts',(-21.0148441174669,-20.114475854294,
12.1067674829437));
#154786=CARTESIAN_POINT('Ctrl Pts',(-21.0529176328921,-20.0397734392993,
12.1109376822935));
#154787=CARTESIAN_POINT('Ctrl Pts',(-21.0873624809752,-19.9631099194739,
12.1151078816433));
#154788=CARTESIAN_POINT('Ctrl Pts',(-21.1179772351408,-19.884873272385,
12.119278080993));
#154789=CARTESIAN_POINT('Ctrl Pts',(-21.1485693987593,-19.8066943559137,
12.1234452031636));
#154790=CARTESIAN_POINT('Ctrl Pts',(-21.1753369141578,-19.7269450449952,
12.1276123253341));
#154791=CARTESIAN_POINT('Ctrl Pts',(-21.1981256703524,-19.6460350716717,
12.1317794475047));
#154792=CARTESIAN_POINT('Ctrl Pts',(-21.2209040463206,-19.5651619526563,
12.1359446715606));
#154793=CARTESIAN_POINT('Ctrl Pts',(-21.2397071410259,-19.4831296648113,
12.1401098956165));
#154794=CARTESIAN_POINT('Ctrl Pts',(-21.2544305326003,-19.4003636139743,
12.1442751196725));
#154795=CARTESIAN_POINT('Ctrl Pts',(-21.2691564647156,-19.3175832817451,
12.1484410624433));
#154796=CARTESIAN_POINT('Ctrl Pts',(-21.2798011983648,-19.2340693856731,
12.1526070052142));
#154797=CARTESIAN_POINT('Ctrl Pts',(-21.2863115236391,-19.1502571216861,
12.1567729479851));
#154798=CARTESIAN_POINT('Ctrl Pts',(-21.2914878410454,-19.0836185341096,
12.1600852620662));
#154799=CARTESIAN_POINT('Ctrl Pts',(-21.2940514917317,-19.0167915973239,
12.1633975761474));
#154800=CARTESIAN_POINT('Ctrl Pts',(-21.2939992159918,-18.9499964727371,
12.1667098902285));
#154801=CARTESIAN_POINT('Ctrl Pts',(-21.2916488572292,-18.9499800095201,
12.1667107986763));
#154802=CARTESIAN_POINT('Ctrl Pts',(-21.2937096036451,-18.6667985676303,
12.1807663462568));
#154803=CARTESIAN_POINT('Ctrl Pts',(-21.1196059381089,-17.531999452779,
12.2372138293977));
#154804=CARTESIAN_POINT('Ctrl Pts',(-19.4558314590011,-16.0122295713503,
12.3360532480991));
#154805=CARTESIAN_POINT('Ctrl Pts',(-16.6528319764031,-16.753811999413,
12.4632290547806));
#154806=CARTESIAN_POINT('Ctrl Pts',(-15.8397231370972,-19.2634826000374,
12.5789421006038));
#154807=CARTESIAN_POINT('Ctrl Pts',(-16.6852502659176,-20.5975253964419,
12.6522632108666));
#154808=CARTESIAN_POINT('Ctrl Pts',(-17.1750494479184,-20.9813915763783,
12.6831923855689));
#154809=CARTESIAN_POINT('Origin',(-18.734,-18.952,-1.76670989022851));
#154810=CARTESIAN_POINT('',(-17.1744641402401,-20.9821349467765,13.549865697334));
#154811=CARTESIAN_POINT('',(-17.1744641402401,-20.9821349467765,13.4833228496967));
#154812=CARTESIAN_POINT('',(-17.1744641402401,-20.9821349467765,-1.76670989022851));
#154813=CARTESIAN_POINT('',(-21.293999998394,-18.9520906788001,13.0332901097364));
#154814=CARTESIAN_POINT('Ctrl Pts',(-21.293999998394,-18.9520906780896,
13.0332901097715));
#154815=CARTESIAN_POINT('Ctrl Pts',(-21.2940031178915,-18.8640218456489,
13.0376462156856));
#154816=CARTESIAN_POINT('Ctrl Pts',(-21.2894573285641,-18.7760356076548,
13.0420023215996));
#154817=CARTESIAN_POINT('Ctrl Pts',(-21.2804139262416,-18.6886065372051,
13.0463584275137));
#154818=CARTESIAN_POINT('Ctrl Pts',(-21.2713470661108,-18.600950683262,
13.0507258327921));
#154819=CARTESIAN_POINT('Ctrl Pts',(-21.2577593163574,-18.5138552818864,
13.0550932380704));
#154820=CARTESIAN_POINT('Ctrl Pts',(-21.2397536148681,-18.4277874271106,
13.0594606433487));
#154821=CARTESIAN_POINT('Ctrl Pts',(-21.2217244341812,-18.3416073409855,
13.0638337436661));
#154822=CARTESIAN_POINT('Ctrl Pts',(-21.1992659159007,-18.25645785704,13.0682068439834));
#154823=CARTESIAN_POINT('Ctrl Pts',(-21.172530963322,-18.1727909517209,
13.0725799443007));
#154824=CARTESIAN_POINT('Ctrl Pts',(-21.1457232584229,-18.0888963683656,
13.0769649448896));
#154825=CARTESIAN_POINT('Ctrl Pts',(-21.114615990053,-18.0064928038113,
13.0813499454785));
#154826=CARTESIAN_POINT('Ctrl Pts',(-21.0794107185113,-17.9260133716796,
13.0857349460673));
#154827=CARTESIAN_POINT('Ctrl Pts',(-21.0474072811094,-17.8528533488881,
13.0897211414781));
#154828=CARTESIAN_POINT('Ctrl Pts',(-21.0120180507083,-17.7812832866316,
13.0937073368888));
#154829=CARTESIAN_POINT('Ctrl Pts',(-20.9734262024016,-17.7116088181557,
13.0976935322996));
#154830=CARTESIAN_POINT('Ctrl Pts',(-20.9329131921061,-17.638465846711,
13.1018781666926));
#154831=CARTESIAN_POINT('Ctrl Pts',(-20.8887375841054,-17.5671736686978,
13.1060628010856));
#154832=CARTESIAN_POINT('Ctrl Pts',(-20.8410930441,-17.4981228031551,13.1102474354787));
#154833=CARTESIAN_POINT('Ctrl Pts',(-20.7935163202,-17.4291702229728,13.1144261135626));
#154834=CARTESIAN_POINT('Ctrl Pts',(-20.742480730941,-17.3624529938654,
13.1186047916466));
#154835=CARTESIAN_POINT('Ctrl Pts',(-20.6882255495789,-17.2983366420662,
13.1227834697305));
#154836=CARTESIAN_POINT('Ctrl Pts',(-20.6329978830833,-17.2330710507404,
13.1270370476159));
#154837=CARTESIAN_POINT('Ctrl Pts',(-20.5744343004285,-17.1705009170565,
13.1312906255014));
#154838=CARTESIAN_POINT('Ctrl Pts',(-20.5128330635405,-17.110980463967,
13.1355442033868));
#154839=CARTESIAN_POINT('Ctrl Pts',(-20.4524260868345,-17.0526139310052,
13.1397153173648));
#154840=CARTESIAN_POINT('Ctrl Pts',(-20.3890985326093,-16.9971802202221,
13.1438864313427));
#154841=CARTESIAN_POINT('Ctrl Pts',(-20.3231707254824,-16.9449782250135,
13.1480575453207));
#154842=CARTESIAN_POINT('Ctrl Pts',(-20.2572650410679,-16.8927937466886,
13.152227259641));
#154843=CARTESIAN_POINT('Ctrl Pts',(-20.1887611969923,-16.8438391155733,
13.1563969739614));
#154844=CARTESIAN_POINT('Ctrl Pts',(-20.1180129698817,-16.7983732683682,
13.1605666882818));
#154845=CARTESIAN_POINT('Ctrl Pts',(-20.0472672602966,-16.752909039033,
13.1647362542258));
#154846=CARTESIAN_POINT('Ctrl Pts',(-19.9742777139364,-16.7109335947648,
13.1689058201699));
#154847=CARTESIAN_POINT('Ctrl Pts',(-19.899426330545,-16.6726620548781,
13.1730753861139));
#154848=CARTESIAN_POINT('Ctrl Pts',(-19.8219432648527,-16.633044934862,
13.1773915488528));
#154849=CARTESIAN_POINT('Ctrl Pts',(-19.7424654713777,-16.5973972639688,
13.1817077115918));
#154850=CARTESIAN_POINT('Ctrl Pts',(-19.6614416802129,-16.5659044592046,
13.1860238743307));
#154851=CARTESIAN_POINT('Ctrl Pts',(-19.5830572305231,-16.5354375292431,
13.1901994385224));
#154852=CARTESIAN_POINT('Ctrl Pts',(-19.5032264199666,-16.508859036806,
13.1943750027141));
#154853=CARTESIAN_POINT('Ctrl Pts',(-19.422371506106,-16.4862861744352,
13.1985505669057));
#154854=CARTESIAN_POINT('Ctrl Pts',(-19.3374328027605,-16.4625732104479,
13.2029370289183));
#154855=CARTESIAN_POINT('Ctrl Pts',(-19.2513643920955,-16.4432812873466,
13.2073234909308));
#154856=CARTESIAN_POINT('Ctrl Pts',(-19.1646662302709,-16.4284852688949,
13.2117099529434));
#154857=CARTESIAN_POINT('Ctrl Pts',(-19.0779680684463,-16.4136892504433,
13.2160964149559));
#154858=CARTESIAN_POINT('Ctrl Pts',(-18.9906407405946,-16.4033891290646,
13.2204828769685));
#154859=CARTESIAN_POINT('Ctrl Pts',(-18.9031862415112,-16.3975967398073,
13.224869338981));
#154860=CARTESIAN_POINT('Ctrl Pts',(-18.8197556535693,-16.3920708669661,
13.2290539733741));
#154861=CARTESIAN_POINT('Ctrl Pts',(-18.7358987953378,-16.3906264585577,
13.2332386077671));
#154862=CARTESIAN_POINT('Ctrl Pts',(-18.6520488590979,-16.3933120529254,
13.2374232421602));
#154863=CARTESIAN_POINT('Ctrl Pts',(-18.5683182728639,-16.3959938246819,
13.2416019202441));
#154864=CARTESIAN_POINT('Ctrl Pts',(-18.4845950449155,-16.4027939079682,
13.2457805983281));
#154865=CARTESIAN_POINT('Ctrl Pts',(-18.4013160390444,-16.413708964259,
13.249959276412));
#154866=CARTESIAN_POINT('Ctrl Pts',(-18.3165443168447,-16.4248196650894,
13.2542128542974));
#154867=CARTESIAN_POINT('Ctrl Pts',(-18.2322333798101,-16.4401943435876,
13.2584664321829));
#154868=CARTESIAN_POINT('Ctrl Pts',(-18.1488425169102,-16.4597739428407,
13.2627200100683));
#154869=CARTESIAN_POINT('Ctrl Pts',(-18.0670683486115,-16.4789739533558,
13.2668911240463));
#154870=CARTESIAN_POINT('Ctrl Pts',(-17.9861793664178,-16.502217188393,
13.2710622380242));
#154871=CARTESIAN_POINT('Ctrl Pts',(-17.9066002780142,-16.5293960909679,
13.2752333520022));
#154872=CARTESIAN_POINT('Ctrl Pts',(-17.8270478931422,-16.5565658733995,
13.2794030663225));
#154873=CARTESIAN_POINT('Ctrl Pts',(-17.7488049640925,-16.587668551974,
13.2835727806429));
#154874=CARTESIAN_POINT('Ctrl Pts',(-17.6722807082305,-16.6225468140603,
13.2877424949633));
#154875=CARTESIAN_POINT('Ctrl Pts',(-17.59575917543,-16.6574238350284,13.2919120609074));
#154876=CARTESIAN_POINT('Ctrl Pts',(-17.52095661247,-16.6960759808161,13.2960816268514));
#154877=CARTESIAN_POINT('Ctrl Pts',(-17.4482606698669,-16.7382984900966,
13.3002511927954));
#154878=CARTESIAN_POINT('Ctrl Pts',(-17.373008827602,-16.7820054907161,
13.3045673555344));
#154879=CARTESIAN_POINT('Ctrl Pts',(-17.3000149555547,-16.8295383292521,
13.3088835182733));
#154880=CARTESIAN_POINT('Ctrl Pts',(-17.2296778491727,-16.8806200574182,
13.3131996810122));
#154881=CARTESIAN_POINT('Ctrl Pts',(-17.1616319666328,-16.9300378036622,
13.3173752452039));
#154882=CARTESIAN_POINT('Ctrl Pts',(-17.0960727569876,-16.9827764479854,
13.3215508093956));
#154883=CARTESIAN_POINT('Ctrl Pts',(-17.0333273206286,-17.0385443727017,
13.3257263735873));
#154884=CARTESIAN_POINT('Ctrl Pts',(-16.9674127614424,-17.0971290027195,
13.3301128355998));
#154885=CARTESIAN_POINT('Ctrl Pts',(-16.904604108851,-17.1590565633928,
13.3344992976123));
#154886=CARTESIAN_POINT('Ctrl Pts',(-16.845234928219,-17.2239471930464,
13.3388857596249));
#154887=CARTESIAN_POINT('Ctrl Pts',(-16.7858657475871,-17.2888378227,13.3432722216374));
#154888=CARTESIAN_POINT('Ctrl Pts',(-16.7299363492649,-17.3566910252288,
13.34765868365));
#154889=CARTESIAN_POINT('Ctrl Pts',(-16.677728404917,-17.4270911085396,
13.3520451456625));
#154890=CARTESIAN_POINT('Ctrl Pts',(-16.6279226254792,-17.4942519796595,
13.3562297800555));
#154891=CARTESIAN_POINT('Ctrl Pts',(-16.5813179797007,-17.5639804959206,
13.3604144144486));
#154892=CARTESIAN_POINT('Ctrl Pts',(-16.5381897594127,-17.6359386840531,
13.3645990488416));
#154893=CARTESIAN_POINT('Ctrl Pts',(-16.495122926808,-17.7077944486114,
13.3687777269256));
#154894=CARTESIAN_POINT('Ctrl Pts',(-16.4555229253635,-17.7818731899369,
13.3729564050095));
#154895=CARTESIAN_POINT('Ctrl Pts',(-16.4196234139922,-17.8578057676358,
13.3771350830935));
#154896=CARTESIAN_POINT('Ctrl Pts',(-16.3830804296802,-17.9350993822182,
13.3813886609789));
#154897=CARTESIAN_POINT('Ctrl Pts',(-16.3503721900681,-18.0143135596365,
13.3856422388643));
#154898=CARTESIAN_POINT('Ctrl Pts',(-16.3216976420463,-18.0950301441644,
13.3898958167498));
#154899=CARTESIAN_POINT('Ctrl Pts',(-16.2935790060916,-18.1741818801958,
13.3940669307277));
#154900=CARTESIAN_POINT('Ctrl Pts',(-16.2693392165557,-18.2547778355446,
13.3982380447057));
#154901=CARTESIAN_POINT('Ctrl Pts',(-16.2491177212504,-18.3364026797034,
13.4024091586836));
#154902=CARTESIAN_POINT('Ctrl Pts',(-16.2289030114633,-18.4180001338574,
13.406578873004));
#154903=CARTESIAN_POINT('Ctrl Pts',(-16.2127040285388,-18.5006253449796,
13.4107485873244));
#154904=CARTESIAN_POINT('Ctrl Pts',(-16.2006099990479,-18.5838490756821,
13.4149183016447));
#154905=CARTESIAN_POINT('Ctrl Pts',(-16.1885163999146,-18.6670698449272,
13.4190878675888));
#154906=CARTESIAN_POINT('Ctrl Pts',(-16.1805275291,-18.7508886360333,13.4232574335328));
#154907=CARTESIAN_POINT('Ctrl Pts',(-16.1766810426043,-18.8348686628405,
13.4274269994769));
#154908=CARTESIAN_POINT('Ctrl Pts',(-16.1726993183887,-18.9218013237896,
13.4317431622158));
#154909=CARTESIAN_POINT('Ctrl Pts',(-16.1731567148618,-19.0089062426187,
13.4360593249547));
#154910=CARTESIAN_POINT('Ctrl Pts',(-16.1780362227548,-19.0956981886122,
13.4403754876936));
#154911=CARTESIAN_POINT('Ctrl Pts',(-16.1827567811915,-19.179662896094,
13.4445510518853));
#154912=CARTESIAN_POINT('Ctrl Pts',(-16.1916156782437,-19.2633342443403,
13.448726616077));
#154913=CARTESIAN_POINT('Ctrl Pts',(-16.2045447628248,-19.3462793465641,
13.4529021802687));
#154914=CARTESIAN_POINT('Ctrl Pts',(-16.2181268647321,-19.4334138087179,
13.4572886422812));
#154915=CARTESIAN_POINT('Ctrl Pts',(-16.236201010622,-19.519746159906,13.4616751042938));
#154916=CARTESIAN_POINT('Ctrl Pts',(-16.2586283495454,-19.6047903125244,
13.4660615663063));
#154917=CARTESIAN_POINT('Ctrl Pts',(-16.2810556884688,-19.6898344651428,
13.4704480283188));
#154918=CARTESIAN_POINT('Ctrl Pts',(-16.3078359712666,-19.7735898897036,
13.4748344903314));
#154919=CARTESIAN_POINT('Ctrl Pts',(-16.3387721302028,-19.8555947386669,
13.4792209523439));
#154920=CARTESIAN_POINT('Ctrl Pts',(-16.3682827836193,-19.9338208908285,
13.4834052908212));
#154921=CARTESIAN_POINT('Ctrl Pts',(-16.4016845822221,-20.0107453980617,
13.4875896292985));
#154922=CARTESIAN_POINT('Ctrl Pts',(-16.438842384675,-20.0859539324045,
13.4917739677759));
#154923=CARTESIAN_POINT('Ctrl Pts',(-16.4759497063984,-20.1610602921992,
13.4959526216205));
#154924=CARTESIAN_POINT('Ctrl Pts',(-16.5168026975527,-20.2344548994179,
13.5001312754651));
#154925=CARTESIAN_POINT('Ctrl Pts',(-16.5612174513804,-20.3057414806432,
13.5043099293097));
#154926=CARTESIAN_POINT('Ctrl Pts',(-16.6055802939412,-20.3769447432318,
13.5084836992093));
#154927=CARTESIAN_POINT('Ctrl Pts',(-16.653496382317,-20.4460444889661,
13.512657469109));
#154928=CARTESIAN_POINT('Ctrl Pts',(-16.704735706151,-20.5126685829187,
13.5168312390086));
#154929=CARTESIAN_POINT('Ctrl Pts',(-16.7559398356268,-20.5792469152951,
13.5210021421032));
#154930=CARTESIAN_POINT('Ctrl Pts',(-16.8104623870239,-20.6433526099033,
13.5251730451978));
#154931=CARTESIAN_POINT('Ctrl Pts',(-16.8680304516944,-20.7046430454591,
13.5293439482923));
#154932=CARTESIAN_POINT('Ctrl Pts',(-16.9255842027873,-20.7659182419165,
13.5335138143442));
#154933=CARTESIAN_POINT('Ctrl Pts',(-16.9861816530085,-20.824379230409,
13.537683680396));
#154934=CARTESIAN_POINT('Ctrl Pts',(-17.0495108542933,-20.8797179041541,
13.5418535464478));
#154935=CARTESIAN_POINT('Ctrl Pts',(-17.0900719586463,-20.9151612332186,
13.5445242634099));
#154936=CARTESIAN_POINT('Ctrl Pts',(-17.1317528860808,-20.949324451798,
13.5471949803719));
#154937=CARTESIAN_POINT('Ctrl Pts',(-17.1744641402401,-20.9821349467765,
13.549865697334));
#154938=CARTESIAN_POINT('Ctrl Pts',(-17.1744641402401,-20.9821349467765,
12.7499597538068));
#154939=CARTESIAN_POINT('Ctrl Pts',(-17.2410532476537,-21.0332882462385,
12.7541315901319));
#154940=CARTESIAN_POINT('Ctrl Pts',(-17.3102191359587,-21.0812059542882,
12.7583034264569));
#154941=CARTESIAN_POINT('Ctrl Pts',(-17.3816116482452,-21.1256250242482,
12.762475262782));
#154942=CARTESIAN_POINT('Ctrl Pts',(-17.4529732632018,-21.1700248704743,
12.7666452936152));
#154943=CARTESIAN_POINT('Ctrl Pts',(-17.5265591985511,-21.2109288425684,
12.7708153244484));
#154944=CARTESIAN_POINT('Ctrl Pts',(-17.6019902058278,-21.2481171193775,
12.7749853552815));
#154945=CARTESIAN_POINT('Ctrl Pts',(-17.6774111955606,-21.2853004574325,
12.7791548323177));
#154946=CARTESIAN_POINT('Ctrl Pts',(-17.7546763576364,-21.3187688776167,
12.7833243093538));
#154947=CARTESIAN_POINT('Ctrl Pts',(-17.8333829516401,-21.3483490839616,
12.78749378639));
#154948=CARTESIAN_POINT('Ctrl Pts',(-17.9121027028482,-21.3779342351631,
12.7916639604283));
#154949=CARTESIAN_POINT('Ctrl Pts',(-17.9922639334031,-21.4036297212893,
12.7958341344665));
#154950=CARTESIAN_POINT('Ctrl Pts',(-18.0734463868029,-21.4253113277734,
12.8000043085048));
#154951=CARTESIAN_POINT('Ctrl Pts',(-18.154718137836,-21.447016783206,12.804179069577));
#154952=CARTESIAN_POINT('Ctrl Pts',(-18.2370129084748,-21.4646994283686,
12.8083538306493));
#154953=CARTESIAN_POINT('Ctrl Pts',(-18.3198983570486,-21.4782857774419,
12.8125285917215));
#154954=CARTESIAN_POINT('Ctrl Pts',(-18.4028354155234,-21.4918805862646,
12.816705952273));
#154955=CARTESIAN_POINT('Ctrl Pts',(-18.486363427206,-21.501373970334,12.8208833128245));
#154956=CARTESIAN_POINT('Ctrl Pts',(-18.5700453931146,-21.5067443877776,
12.825060673376));
#154957=CARTESIAN_POINT('Ctrl Pts',(-18.6538651895487,-21.5121236507048,
12.8292449143563));
#154958=CARTESIAN_POINT('Ctrl Pts',(-18.7378389869997,-21.5133663857226,
12.8334291553365));
#154959=CARTESIAN_POINT('Ctrl Pts',(-18.8215306928142,-21.5105031518088,
12.8376133963167));
#154960=CARTESIAN_POINT('Ctrl Pts',(-18.8597239861841,-21.5091964950524,
12.8395229038567));
#154961=CARTESIAN_POINT('Ctrl Pts',(-18.8978586153629,-21.5070354359871,
12.8414324113967));
#154962=CARTESIAN_POINT('Ctrl Pts',(-18.9358937423124,-21.5040264334084,
12.8433419189367));
#154963=CARTESIAN_POINT('Ctrl Pts',(-19.0192466995766,-21.497432285223,
12.8475265533297));
#154964=CARTESIAN_POINT('Ctrl Pts',(-19.1024313715337,-21.4867379250515,
12.8517111877228));
#154965=CARTESIAN_POINT('Ctrl Pts',(-19.1850120996547,-21.4719579532137,
12.8558958221158));
#154966=CARTESIAN_POINT('Ctrl Pts',(-19.2674752843307,-21.4571990188365,
12.8600745001998));
#154967=CARTESIAN_POINT('Ctrl Pts',(-19.3493357837206,-21.4383661042867,
12.8642531782837));
#154968=CARTESIAN_POINT('Ctrl Pts',(-19.4301618064492,-21.4155256725355,
12.8684318563676));
#154969=CARTESIAN_POINT('Ctrl Pts',(-19.5124365775465,-21.3922758424603,
12.8726854342531));
#154970=CARTESIAN_POINT('Ctrl Pts',(-19.5936389405807,-21.3648734505894,
12.8769390121385));
#154971=CARTESIAN_POINT('Ctrl Pts',(-19.6733229700786,-21.333443335014,
12.881192590024));
#154972=CARTESIAN_POINT('Ctrl Pts',(-19.7514621691741,-21.3026225535599,
12.8853637040019));
#154973=CARTESIAN_POINT('Ctrl Pts',(-19.8281409334345,-21.2679290018995,
12.8895348179798));
#154974=CARTESIAN_POINT('Ctrl Pts',(-19.9029545672468,-21.229530509063,
12.8937059319578));
#154975=CARTESIAN_POINT('Ctrl Pts',(-19.9777430966217,-21.1911449012117,
12.8978756462782));
#154976=CARTESIAN_POINT('Ctrl Pts',(-20.0506673295888,-21.149057031143,
12.9020453605985));
#154977=CARTESIAN_POINT('Ctrl Pts',(-20.1213450915268,-21.1034817212834,
12.9062150749189));
#154978=CARTESIAN_POINT('Ctrl Pts',(-20.1920203384466,-21.0579080331889,
12.9103846408629));
#154979=CARTESIAN_POINT('Ctrl Pts',(-20.2604488871165,-21.008847402065,
12.914554206807));
#154980=CARTESIAN_POINT('Ctrl Pts',(-20.3262767630685,-20.9565584825073,
12.918723772751));
#154981=CARTESIAN_POINT('Ctrl Pts',(-20.3944190659317,-20.9024311490432,
12.9230399354899));
#154982=CARTESIAN_POINT('Ctrl Pts',(-20.4597740011395,-20.8448446181548,
12.9273560982289));
#154983=CARTESIAN_POINT('Ctrl Pts',(-20.521987002802,-20.7841305842682,
12.9316722609678));
#154984=CARTESIAN_POINT('Ctrl Pts',(-20.582173422479,-20.7253943036496,
12.9358478251595));
#154985=CARTESIAN_POINT('Ctrl Pts',(-20.63941917621,-20.6637315251353,12.9400233893512));
#154986=CARTESIAN_POINT('Ctrl Pts',(-20.6934427607502,-20.5994780931301,
12.9441989535428));
#154987=CARTESIAN_POINT('Ctrl Pts',(-20.7501949481167,-20.5319793730223,
12.9485854155554));
#154988=CARTESIAN_POINT('Ctrl Pts',(-20.803390556233,-20.4616218795445,
12.9529718775679));
#154989=CARTESIAN_POINT('Ctrl Pts',(-20.852754442665,-20.3888297086597,
12.9573583395805));
#154990=CARTESIAN_POINT('Ctrl Pts',(-20.9021183290971,-20.316037537775,
12.961744801593));
#154991=CARTESIAN_POINT('Ctrl Pts',(-20.9476502584794,-20.240811225245,
12.9661312636056));
#154992=CARTESIAN_POINT('Ctrl Pts',(-20.9891316170535,-20.1636028184871,
12.9705177256181));
#154993=CARTESIAN_POINT('Ctrl Pts',(-21.0308618762442,-20.0859311380874,
12.9749305077209));
#154994=CARTESIAN_POINT('Ctrl Pts',(-21.0686351706121,-20.0059905501583,
12.9793432898236));
#154995=CARTESIAN_POINT('Ctrl Pts',(-21.1022126120118,-19.9241980375974,
12.9837560719264));
#154996=CARTESIAN_POINT('Ctrl Pts',(-21.1356929152447,-19.8426421474353,
12.9881560880307));
#154997=CARTESIAN_POINT('Ctrl Pts',(-21.1650014030469,-19.759245362016,
12.9925561041351));
#154998=CARTESIAN_POINT('Ctrl Pts',(-21.1899457627449,-19.6744475139796,
12.9969561202394));
#154999=CARTESIAN_POINT('Ctrl Pts',(-21.2148467487816,-19.5897971138308,
13.0013484855236));
#155000=CARTESIAN_POINT('Ctrl Pts',(-21.235398596884,-19.5037508664335,
13.0057408508078));
#155001=CARTESIAN_POINT('Ctrl Pts',(-21.2514572537729,-19.4167676574658,
13.0101332160921));
#155002=CARTESIAN_POINT('Ctrl Pts',(-21.2674789983323,-19.3299843875645,
13.0145154851126));
#155003=CARTESIAN_POINT('Ctrl Pts',(-21.2790280568698,-19.2422688247272,
13.0188977541331));
#155004=CARTESIAN_POINT('Ctrl Pts',(-21.2860106924303,-19.1540926166924,
13.0232800231537));
#155005=CARTESIAN_POINT('Ctrl Pts',(-21.2913273283411,-19.0869545296399,
13.0266167186812));
#155006=CARTESIAN_POINT('Ctrl Pts',(-21.2939976088987,-19.0195497546626,
13.0299534142088));
#155007=CARTESIAN_POINT('Ctrl Pts',(-21.293999998394,-18.9520906788001,
13.0332901097364));
#155008=CARTESIAN_POINT('',(-21.2943301210028,-18.9513574887884,12.9667098341108));
#155009=CARTESIAN_POINT('Ctrl Pts',(-17.1750494479184,-20.9813915763783,
12.6831923855689));
#155010=CARTESIAN_POINT('Ctrl Pts',(-17.356575497218,-21.1236574552614,
12.6946551464271));
#155011=CARTESIAN_POINT('Ctrl Pts',(-18.2953377646256,-21.6766232007702,
12.7485098428457));
#155012=CARTESIAN_POINT('Ctrl Pts',(-20.4360628533385,-21.4324759086211,
12.8430154491812));
#155013=CARTESIAN_POINT('Ctrl Pts',(-21.2952859035193,-19.7651270969621,
12.9260582946585));
#155014=CARTESIAN_POINT('Ctrl Pts',(-21.2980343668152,-18.9513691597422,
12.9667092045753));
#155015=CARTESIAN_POINT('Ctrl Pts',(-21.2939999191096,-18.9513564484225,
12.9667098902285));
#155016=CARTESIAN_POINT('Ctrl Pts',(-21.2939911726516,-18.9165636940744,
12.9684506873211));
#155017=CARTESIAN_POINT('Ctrl Pts',(-21.2932731600888,-18.881780730387,
12.9701914844137));
#155018=CARTESIAN_POINT('Ctrl Pts',(-21.2918468828523,-18.8470270326106,
12.9719322815063));
#155019=CARTESIAN_POINT('Ctrl Pts',(-21.2884183105029,-18.7634839708603,
12.9761169158993));
#155020=CARTESIAN_POINT('Ctrl Pts',(-21.2808860937369,-18.6799535889704,
12.9803015502924));
#155021=CARTESIAN_POINT('Ctrl Pts',(-21.2692483017375,-18.5968717857769,
12.9844861846854));
#155022=CARTESIAN_POINT('Ctrl Pts',(-21.2576270746945,-18.5139082392468,
12.9886648627694));
#155023=CARTESIAN_POINT('Ctrl Pts',(-21.2419119432712,-18.4313924548469,
12.9928435408533));
#155024=CARTESIAN_POINT('Ctrl Pts',(-21.2221529486457,-18.3497584337279,
12.9970222189372));
#155025=CARTESIAN_POINT('Ctrl Pts',(-21.2020397882419,-18.2666611814494,
13.0012757968227));
#155026=CARTESIAN_POINT('Ctrl Pts',(-21.1777363859676,-18.1844780963255,
13.0055293747081));
#155027=CARTESIAN_POINT('Ctrl Pts',(-21.1493505801536,-18.1036595170853,
13.0097829525935));
#155028=CARTESIAN_POINT('Ctrl Pts',(-21.1215150885756,-18.0244077637083,
13.0139540665715));
#155029=CARTESIAN_POINT('Ctrl Pts',(-21.0897542310845,-17.9464685351597,
13.0181251805494));
#155030=CARTESIAN_POINT('Ctrl Pts',(-21.0542203695086,-17.8702526002261,
13.0222962945274));
#155031=CARTESIAN_POINT('Ctrl Pts',(-21.0186984316631,-17.7940622402855,
13.0264660088478));
#155032=CARTESIAN_POINT('Ctrl Pts',(-20.9794061983924,-17.7195944421082,
13.0306357231681));
#155033=CARTESIAN_POINT('Ctrl Pts',(-20.9365438451406,-17.6472392517272,
13.0348054374885));
#155034=CARTESIAN_POINT('Ctrl Pts',(-20.8936830171152,-17.5748866360543,
13.0389750034325));
#155035=CARTESIAN_POINT('Ctrl Pts',(-20.8472525568965,-17.5046468740728,
13.0431445693766));
#155036=CARTESIAN_POINT('Ctrl Pts',(-20.7974975099507,-17.4368834941077,
13.0473141353206));
#155037=CARTESIAN_POINT('Ctrl Pts',(-20.7459931369336,-17.366737637298,
13.0516302980595));
#155038=CARTESIAN_POINT('Ctrl Pts',(-20.6909263546122,-17.2992459668448,
13.0559464607985));
#155039=CARTESIAN_POINT('Ctrl Pts',(-20.6326151733211,-17.234775371818,
13.0602626235374));
#155040=CARTESIAN_POINT('Ctrl Pts',(-20.5762034726275,-17.1724048996433,
13.0644381877291));
#155041=CARTESIAN_POINT('Ctrl Pts',(-20.5167558657732,-17.1128620023875,
13.0686137519208));
#155042=CARTESIAN_POINT('Ctrl Pts',(-20.4545972806997,-17.0564407163983,
13.0727893161124));
#155043=CARTESIAN_POINT('Ctrl Pts',(-20.3892992132619,-16.9971697253824,
13.077175778125));
#155044=CARTESIAN_POINT('Ctrl Pts',(-20.3210095593889,-16.9413443477726,
13.0815622401375));
#155045=CARTESIAN_POINT('Ctrl Pts',(-20.2501416763133,-16.889255610274,
13.0859487021501));
#155046=CARTESIAN_POINT('Ctrl Pts',(-20.1792737932376,-16.8371668727754,
13.0903351641627));
#155047=CARTESIAN_POINT('Ctrl Pts',(-20.1058282074104,-16.7888150309008,
13.0947216261752));
#155048=CARTESIAN_POINT('Ctrl Pts',(-20.0302483510417,-16.7444356832877,
13.0991080881878));
#155049=CARTESIAN_POINT('Ctrl Pts',(-19.958146035901,-16.7020982952443,
13.1032927225808));
#155050=CARTESIAN_POINT('Ctrl Pts',(-19.8838331576254,-16.6632182861073,
13.1074773569739));
#155051=CARTESIAN_POINT('Ctrl Pts',(-19.8076751930389,-16.6280332231607,
13.1116619913669));
#155052=CARTESIAN_POINT('Ctrl Pts',(-19.7316256298885,-16.5928982417961,
13.1158406694508));
#155053=CARTESIAN_POINT('Ctrl Pts',(-19.6537366110356,-16.5614479512896,
13.1200193475348));
#155054=CARTESIAN_POINT('Ctrl Pts',(-19.5744001491065,-16.533875191521,
13.1241980256187));
#155055=CARTESIAN_POINT('Ctrl Pts',(-19.4936416381154,-16.5058082098496,
13.1284516035042));
#155056=CARTESIAN_POINT('Ctrl Pts',(-19.4113836985809,-16.4817593798136,
13.1327051813896));
#155057=CARTESIAN_POINT('Ctrl Pts',(-19.3280633649497,-16.461881786255,
13.136958759275));
#155058=CARTESIAN_POINT('Ctrl Pts',(-19.2463583585721,-16.4423895586354,
13.141129873253));
#155059=CARTESIAN_POINT('Ctrl Pts',(-19.1636322517454,-16.4269083873419,
13.1453009872309));
#155060=CARTESIAN_POINT('Ctrl Pts',(-19.0803129065813,-16.4155325015417,
13.1494721012089));
#155061=CARTESIAN_POINT('Ctrl Pts',(-18.9970215200281,-16.4041604330299,
13.1536418155293));
#155062=CARTESIAN_POINT('Ctrl Pts',(-18.9131377459123,-16.39689097632,13.1578115298496));
#155063=CARTESIAN_POINT('Ctrl Pts',(-18.8290979023925,-16.3937669400618,
13.16198124417));
#155064=CARTESIAN_POINT('Ctrl Pts',(-18.745061049371,-16.3906430149703,
13.1661508101141));
#155065=CARTESIAN_POINT('Ctrl Pts',(-18.6608685977347,-16.3916642332765,
13.1703203760581));
#155066=CARTESIAN_POINT('Ctrl Pts',(-18.5769588557387,-16.3968213215102,
13.1744899420021));
#155067=CARTESIAN_POINT('Ctrl Pts',(-18.4900989507281,-16.4021597266041,
13.1788061047411));
#155068=CARTESIAN_POINT('Ctrl Pts',(-18.4035425318192,-16.4119302148937,
13.18312226748));
#155069=CARTESIAN_POINT('Ctrl Pts',(-18.317770227621,-16.4260639801085,
13.1874384302189));
#155070=CARTESIAN_POINT('Ctrl Pts',(-18.2347919472103,-16.4397373394081,
13.1916139944106));
#155071=CARTESIAN_POINT('Ctrl Pts',(-18.1525479314087,-16.4574939280206,
13.1957895586023));
#155072=CARTESIAN_POINT('Ctrl Pts',(-18.0714612955844,-16.4792196892665,
13.1999651227939));
#155073=CARTESIAN_POINT('Ctrl Pts',(-17.9862791665499,-16.5020427670648,
13.2043515848065));
#155074=CARTESIAN_POINT('Ctrl Pts',(-17.9023749641123,-16.5292463408116,
13.208738046819));
#155075=CARTESIAN_POINT('Ctrl Pts',(-17.8202171381047,-16.5606403697255,
13.2131245088315));
#155076=CARTESIAN_POINT('Ctrl Pts',(-17.7380593120971,-16.5920343986394,
13.2175109708441));
#155077=CARTESIAN_POINT('Ctrl Pts',(-17.6576483623233,-16.6276185783625,
13.2218974328566));
#155078=CARTESIAN_POINT('Ctrl Pts',(-17.579422411398,-16.6671475776545,
13.2262838948691));
#155079=CARTESIAN_POINT('Ctrl Pts',(-17.5047957524333,-16.7048577890932,
13.2304685292622));
#155080=CARTESIAN_POINT('Ctrl Pts',(-17.4318796660886,-16.7462981479269,
13.2346531636552));
#155081=CARTESIAN_POINT('Ctrl Pts',(-17.3610717345267,-16.7912899366494,
13.2388377980483));
#155082=CARTESIAN_POINT('Ctrl Pts',(-17.2903645892912,-16.8362176851296,
13.2430164761322));
#155083=CARTESIAN_POINT('Ctrl Pts',(-17.2217600234685,-16.8846865780311,
13.2471951542162));
#155084=CARTESIAN_POINT('Ctrl Pts',(-17.1556323738796,-16.9364713753421,
13.2513738323001));
#155085=CARTESIAN_POINT('Ctrl Pts',(-17.0883194336969,-16.989184377928,
13.2556274101856));
#155086=CARTESIAN_POINT('Ctrl Pts',(-17.0235735109215,-17.045333111899,
13.259880988071));
#155087=CARTESIAN_POINT('Ctrl Pts',(-16.9617598841366,-17.1046329623693,
13.2641345659564));
#155088=CARTESIAN_POINT('Ctrl Pts',(-16.9011446351263,-17.1627831695241,
13.2683056799344));
#155089=CARTESIAN_POINT('Ctrl Pts',(-16.8433493474163,-17.2239630692775,
13.2724767939123));
#155090=CARTESIAN_POINT('Ctrl Pts',(-16.7886848464703,-17.2878639017653,
13.2766479078903));
#155091=CARTESIAN_POINT('Ctrl Pts',(-16.7340386887256,-17.3517432917117,
13.2808176222107));
#155092=CARTESIAN_POINT('Ctrl Pts',(-16.6825215301017,-17.4183414518072,
13.284987336531));
#155093=CARTESIAN_POINT('Ctrl Pts',(-16.6344055366424,-17.4873146790392,
13.2891570508514));
#155094=CARTESIAN_POINT('Ctrl Pts',(-16.5862912553567,-17.5562854519078,
13.2933266167954));
#155095=CARTESIAN_POINT('Ctrl Pts',(-16.5415781611062,-17.6276307460898,
13.2974961827395));
#155096=CARTESIAN_POINT('Ctrl Pts',(-16.5004957043155,-17.7009769941529,
13.3016657486835));
#155097=CARTESIAN_POINT('Ctrl Pts',(-16.4579688390246,-17.7769020058155,
13.3059819114224));
#155098=CARTESIAN_POINT('Ctrl Pts',(-16.4193329255797,-17.8549708362668,
13.3102980741614));
#155099=CARTESIAN_POINT('Ctrl Pts',(-16.3847902639464,-17.934742109379,
13.3146142369003));
#155100=CARTESIAN_POINT('Ctrl Pts',(-16.3513728258825,-18.0119148416598,
13.318789801092));
#155101=CARTESIAN_POINT('Ctrl Pts',(-16.3217861809923,-18.0906803481869,
13.3229653652836));
#155102=CARTESIAN_POINT('Ctrl Pts',(-16.2961634499818,-18.1706211191776,
13.3271409294753));
#155103=CARTESIAN_POINT('Ctrl Pts',(-16.2692465757401,-18.2545995084699,
13.3315273914879));
#155104=CARTESIAN_POINT('Ctrl Pts',(-16.2467047227919,-18.3398744431048,
13.3359138535004));
#155105=CARTESIAN_POINT('Ctrl Pts',(-16.2286316599242,-18.4259491654359,
13.340300315513));
#155106=CARTESIAN_POINT('Ctrl Pts',(-16.2105585970564,-18.5120238877669,
13.3446867775255));
#155107=CARTESIAN_POINT('Ctrl Pts',(-16.1969543388866,-18.598897812795,
13.3490732395381));
#155108=CARTESIAN_POINT('Ctrl Pts',(-16.1878497481281,-18.6860697555883,
13.3534597015506));
#155109=CARTESIAN_POINT('Ctrl Pts',(-16.1791640730867,-18.7692307880738,
13.3576443359436));
#155110=CARTESIAN_POINT('Ctrl Pts',(-16.1745407622114,-18.852972557727,
13.3618289703367));
#155111=CARTESIAN_POINT('Ctrl Pts',(-16.1740447460464,-18.9368640244712,
13.3660136047297));
#155112=CARTESIAN_POINT('Ctrl Pts',(-16.173549435899,-19.0206360820962,
13.3701922828137));
#155113=CARTESIAN_POINT('Ctrl Pts',(-16.1771697541693,-19.1045569574875,
13.3743709608976));
#155114=CARTESIAN_POINT('Ctrl Pts',(-16.1849189310737,-19.1881899744725,
13.3785496389816));
#155115=CARTESIAN_POINT('Ctrl Pts',(-16.1928070064048,-19.2733220531809,
13.382803216867));
#155116=CARTESIAN_POINT('Ctrl Pts',(-16.2049734659499,-19.3581553727241,
13.3870567947524));
#155117=CARTESIAN_POINT('Ctrl Pts',(-16.2213767120001,-19.4422287349806,
13.3913103726379));
#155118=CARTESIAN_POINT('Ctrl Pts',(-16.2374619491174,-19.5246721710542,
13.3954814866158));
#155119=CARTESIAN_POINT('Ctrl Pts',(-16.2576210698179,-19.6063843810837,
13.3996526005938));
#155120=CARTESIAN_POINT('Ctrl Pts',(-16.2817626998464,-19.686936884185,
13.4038237145717));
#155121=CARTESIAN_POINT('Ctrl Pts',(-16.3058962289179,-19.767462357116,
13.4079934288921));
#155122=CARTESIAN_POINT('Ctrl Pts',(-16.334009481308,-19.8468284556772,
13.4121631432125));
#155123=CARTESIAN_POINT('Ctrl Pts',(-16.3659607754928,-19.9246202913754,
13.4163328575329));
#155124=CARTESIAN_POINT('Ctrl Pts',(-16.3979109327134,-20.0024093589062,
13.4205024234769));
#155125=CARTESIAN_POINT('Ctrl Pts',(-16.4336986846161,-20.0786238497405,
13.4246719894209));
#155126=CARTESIAN_POINT('Ctrl Pts',(-16.4731341172713,-20.1528686274167,
13.428841555365));
#155127=CARTESIAN_POINT('Ctrl Pts',(-16.5139560510899,-20.2297237598851,
13.4331577181039));
#155128=CARTESIAN_POINT('Ctrl Pts',(-16.5586866956795,-20.3044676260571,
13.4374738808428));
#155129=CARTESIAN_POINT('Ctrl Pts',(-16.6070644247003,-20.3766912151497,
13.4417900435817));
#155130=CARTESIAN_POINT('Ctrl Pts',(-16.6538662542868,-20.4465621284242,
13.4459656077734));
#155131=CARTESIAN_POINT('Ctrl Pts',(-16.7040808906406,-20.5140740893659,
13.4501411719651));
#155132=CARTESIAN_POINT('Ctrl Pts',(-16.75742932982,-20.5788891744013,13.4543167361568));
#155133=CARTESIAN_POINT('Ctrl Pts',(-16.8134722718384,-20.6469779152985,
13.4587031981693));
#155134=CARTESIAN_POINT('Ctrl Pts',(-16.8729735193545,-20.7120897510531,
13.4630896601819));
#155135=CARTESIAN_POINT('Ctrl Pts',(-16.9355661330672,-20.7738769514621,
13.4674761221944));
#155136=CARTESIAN_POINT('Ctrl Pts',(-16.9981587467798,-20.8356641518712,
13.4718625842069));
#155137=CARTESIAN_POINT('Ctrl Pts',(-17.0638422427094,-20.8941263879947,
13.4762490462195));
#155138=CARTESIAN_POINT('Ctrl Pts',(-17.1322119090441,-20.9489664272771,
13.480635508232));
#155139=CARTESIAN_POINT('Ctrl Pts',(-17.1461740071802,-20.9601655752516,
13.4815312887202));
#155140=CARTESIAN_POINT('Ctrl Pts',(-17.160259106387,-20.9712227363748,
13.4824270692085));
#155141=CARTESIAN_POINT('Ctrl Pts',(-17.1744641402401,-20.9821349467765,
13.4833228496967));
#155142=CARTESIAN_POINT('Origin',(-18.734,-18.952,-1.76670989022851));
#155143=CARTESIAN_POINT('',(-17.1732300411181,-20.9837128798172,14.34978651614));
#155144=CARTESIAN_POINT('',(-17.1756294737623,-20.9805869941177,14.2834124255784));
#155145=CARTESIAN_POINT('',(-17.1744641402401,-20.9821349467765,-1.76670989022851));
#155146=CARTESIAN_POINT('',(-21.2939989424941,-18.949673107456,13.8332901097715));
#155147=CARTESIAN_POINT('Ctrl Pts',(-21.294449633852,-18.9496726978033,
13.8332901097715));
#155148=CARTESIAN_POINT('Ctrl Pts',(-21.2961551522482,-18.7657813487039,
13.8424428639771));
#155149=CARTESIAN_POINT('Ctrl Pts',(-21.1940976782198,-17.7320561538789,
13.8939875537431));
#155150=CARTESIAN_POINT('Ctrl Pts',(-19.7898862958127,-16.1150306505046,
13.9879241790696));
#155151=CARTESIAN_POINT('Ctrl Pts',(-16.9200889626634,-16.5285690213481,
14.1150999857511));
#155152=CARTESIAN_POINT('Ctrl Pts',(-15.7765851098014,-19.0295417863752,
14.2357207647745));
#155153=CARTESIAN_POINT('Ctrl Pts',(-16.6072658624459,-20.5404052968016,
14.3139496082375));
#155154=CARTESIAN_POINT('Ctrl Pts',(-17.1732300411181,-20.9837128798172,
14.34978651614));
#155155=CARTESIAN_POINT('Ctrl Pts',(-17.1744641402401,-20.9821349467765,
13.549865697334));
#155156=CARTESIAN_POINT('Ctrl Pts',(-17.2411542319938,-21.0333658217219,
13.5540358010398));
#155157=CARTESIAN_POINT('Ctrl Pts',(-17.3103575700477,-21.0812964944487,
13.5582059047456));
#155158=CARTESIAN_POINT('Ctrl Pts',(-17.3817085509902,-21.1256853123061,
13.5623760084514));
#155159=CARTESIAN_POINT('Ctrl Pts',(-17.4531373470503,-21.1701225404449,
13.5665506600569));
#155160=CARTESIAN_POINT('Ctrl Pts',(-17.5267180697703,-21.211009960323,
13.5707253116625));
#155161=CARTESIAN_POINT('Ctrl Pts',(-17.6020587050214,-21.2481508889274,
13.5748999632681));
#155162=CARTESIAN_POINT('Ctrl Pts',(-17.6774451458419,-21.2853143984588,
13.5790771529766));
#155163=CARTESIAN_POINT('Ctrl Pts',(-17.7545932070973,-21.3187266999457,
13.5832543426852));
#155164=CARTESIAN_POINT('Ctrl Pts',(-17.8330912166259,-21.3482394212681,
13.5874315323938));
#155165=CARTESIAN_POINT('Ctrl Pts',(-17.9117197868307,-21.3778012291964,
13.5916156697526));
#155166=CARTESIAN_POINT('Ctrl Pts',(-17.9917023498214,-21.4034503690721,
13.5957998071114));
#155167=CARTESIAN_POINT('Ctrl Pts',(-18.0726128098124,-21.4250885517215,
13.5999839444702));
#155168=CARTESIAN_POINT('Ctrl Pts',(-18.1139485923167,-21.4361431324504,
13.6021215493219));
#155169=CARTESIAN_POINT('Ctrl Pts',(-18.1555264006885,-21.4461516743427,
13.6042591541736));
#155170=CARTESIAN_POINT('Ctrl Pts',(-18.1972887614197,-21.4551062794819,
13.6063967590253));
#155171=CARTESIAN_POINT('Ctrl Pts',(-18.2790439141132,-21.4726360622251,
13.6105813934184));
#155172=CARTESIAN_POINT('Ctrl Pts',(-18.3618109357872,-21.4861888889159,
13.6147660278114));
#155173=CARTESIAN_POINT('Ctrl Pts',(-18.4451682027607,-21.4956541024486,
13.6189506622045));
#155174=CARTESIAN_POINT('Ctrl Pts',(-18.5284068209824,-21.5051058434214,
13.6231293402884));
#155175=CARTESIAN_POINT('Ctrl Pts',(-18.6122335625332,-21.5104814765754,
13.6273080183723));
#155176=CARTESIAN_POINT('Ctrl Pts',(-18.6962156707041,-21.5117211458398,
13.6314866964563));
#155177=CARTESIAN_POINT('Ctrl Pts',(-18.781703097807,-21.5129830352849,
13.6357402743417));
#155178=CARTESIAN_POINT('Ctrl Pts',(-18.8673510447846,-21.5099591270341,
13.6399938522272));
#155179=CARTESIAN_POINT('Ctrl Pts',(-18.9526965098739,-21.5026414559026,
13.6442474301126));
#155180=CARTESIAN_POINT('Ctrl Pts',(-19.0363873865845,-21.4954656521053,
13.6484185440906));
#155181=CARTESIAN_POINT('Ctrl Pts',(-19.1197869256883,-21.4841611267896,
13.6525896580685));
#155182=CARTESIAN_POINT('Ctrl Pts',(-19.2024593315003,-21.4687729048785,
13.6567607720465));
#155183=CARTESIAN_POINT('Ctrl Pts',(-19.285103995788,-21.4533898466338,
13.6609304863668));
#155184=CARTESIAN_POINT('Ctrl Pts',(-19.3670215594764,-21.4339258973909,
13.6651002006872));
#155185=CARTESIAN_POINT('Ctrl Pts',(-19.4477843610412,-21.4104775544904,
13.6692699150076));
#155186=CARTESIAN_POINT('Ctrl Pts',(-19.5285442887191,-21.3870300459825,
13.6734394809516));
#155187=CARTESIAN_POINT('Ctrl Pts',(-19.6081490944219,-21.3595985548015,
13.6776090468957));
#155188=CARTESIAN_POINT('Ctrl Pts',(-19.6861855970018,-21.3283296465058,
13.6817786128397));
#155189=CARTESIAN_POINT('Ctrl Pts',(-19.7669657667439,-21.2959613619688,
13.6860947755787));
#155190=CARTESIAN_POINT('Ctrl Pts',(-19.846064808783,-21.2594809885573,
13.6904109383176));
#155191=CARTESIAN_POINT('Ctrl Pts',(-19.9230480777106,-21.2191049091061,
13.6947271010565));
#155192=CARTESIAN_POINT('Ctrl Pts',(-19.9975236247501,-21.1800440761961,
13.6989026652482));
#155193=CARTESIAN_POINT('Ctrl Pts',(-20.070018742585,-21.1373377246258,
13.7030782294399));
#155194=CARTESIAN_POINT('Ctrl Pts',(-20.1401676067986,-21.0912271178139,
13.7072537936316));
#155195=CARTESIAN_POINT('Ctrl Pts',(-20.2138595233805,-21.0427875738695,
13.7116402556441));
#155196=CARTESIAN_POINT('Ctrl Pts',(-20.2849614681667,-20.990591184541,
13.7160267176566));
#155197=CARTESIAN_POINT('Ctrl Pts',(-20.3530884618269,-20.9349655954602,
13.7204131796692));
#155198=CARTESIAN_POINT('Ctrl Pts',(-20.4212154554872,-20.8793400063795,
13.7247996416817));
#155199=CARTESIAN_POINT('Ctrl Pts',(-20.4863671192075,-20.8202856635707,
13.7291861036943));
#155200=CARTESIAN_POINT('Ctrl Pts',(-20.548204641978,-20.7581731691688,
13.7335725657068));
#155201=CARTESIAN_POINT('Ctrl Pts',(-20.6067777194386,-20.6993396360183,
13.7377274633762));
#155202=CARTESIAN_POINT('Ctrl Pts',(-20.6626103382647,-20.6375286216454,
13.7418823610455));
#155203=CARTESIAN_POINT('Ctrl Pts',(-20.7153787245626,-20.5730300274365,
13.7460372587149));
#155204=CARTESIAN_POINT('Ctrl Pts',(-20.7677053791601,-20.5090713601742,
13.7501573751423));
#155205=CARTESIAN_POINT('Ctrl Pts',(-20.8170185699061,-20.4424702805591,
13.7542774915697));
#155206=CARTESIAN_POINT('Ctrl Pts',(-20.8630375889924,-20.3735480803185,
13.7583976079971));
#155207=CARTESIAN_POINT('Ctrl Pts',(-20.909012526032,-20.3046919012951,
13.7625137777266));
#155208=CARTESIAN_POINT('Ctrl Pts',(-20.9516992900879,-20.233519404422,
13.7666299474561));
#155209=CARTESIAN_POINT('Ctrl Pts',(-20.9908578231796,-20.1603843618457,
13.7707461171856));
#155210=CARTESIAN_POINT('Ctrl Pts',(-21.0299913601116,-20.0872960037352,
13.7748596594307));
#155211=CARTESIAN_POINT('Ctrl Pts',(-21.0656009133713,-20.0122480031423,
13.7789732016758));
#155212=CARTESIAN_POINT('Ctrl Pts',(-21.0974909394085,-19.9356211564083,
13.7830867439209));
#155213=CARTESIAN_POINT('Ctrl Pts',(-21.1299241917561,-19.8576890200775,
13.7872703577418));
#155214=CARTESIAN_POINT('Ctrl Pts',(-21.158509766141,-19.7781241832438,
13.7914539715627));
#155215=CARTESIAN_POINT('Ctrl Pts',(-21.1830923574769,-19.6973500013741,
13.7956375853835));
#155216=CARTESIAN_POINT('Ctrl Pts',(-21.2072638620763,-19.6179265800633,
13.7997512379815));
#155217=CARTESIAN_POINT('Ctrl Pts',(-21.227565151866,-19.5373344318,13.8038648905795));
#155218=CARTESIAN_POINT('Ctrl Pts',(-21.2438990336339,-19.4559909135726,
13.8079785431775));
#155219=CARTESIAN_POINT('Ctrl Pts',(-21.260649602877,-19.372572271641,13.8121971376098));
#155220=CARTESIAN_POINT('Ctrl Pts',(-21.2732274574716,-19.2883639128976,
13.8164157320421));
#155221=CARTESIAN_POINT('Ctrl Pts',(-21.2815840465261,-19.2038243949373,
13.8206343264745));
#155222=CARTESIAN_POINT('Ctrl Pts',(-21.2899406355806,-19.119284876977,
13.8248529209068));
#155223=CARTESIAN_POINT('Ctrl Pts',(-21.2940759677847,-19.0344147354448,
13.8290715153392));
#155224=CARTESIAN_POINT('Ctrl Pts',(-21.2939989424941,-18.949673107456,
13.8332901097715));
#155225=CARTESIAN_POINT('',(-21.2939989173812,-18.9543543592142,13.7667098774877));
#155226=CARTESIAN_POINT('Ctrl Pts',(-17.1744641402401,-20.9821349467765,
13.4833228496967));
#155227=CARTESIAN_POINT('Ctrl Pts',(-17.2408008210132,-21.0330943338099,
13.4875060924052));
#155228=CARTESIAN_POINT('Ctrl Pts',(-17.3097559456157,-21.0808895947018,
13.4916893351137));
#155229=CARTESIAN_POINT('Ctrl Pts',(-17.3809948073905,-21.1252411161148,
13.4958725778222));
#155230=CARTESIAN_POINT('Ctrl Pts',(-17.4521373200177,-21.1695326529747,
13.5000501627779));
#155231=CARTESIAN_POINT('Ctrl Pts',(-17.5255570468011,-21.2103894610906,
13.5042277477337));
#155232=CARTESIAN_POINT('Ctrl Pts',(-17.6008876366303,-21.2475732120711,
13.5084053326894));
#155233=CARTESIAN_POINT('Ctrl Pts',(-17.6761382792445,-21.2847175004996,
13.5125784840374));
#155234=CARTESIAN_POINT('Ctrl Pts',(-17.7532953436455,-21.3181962768837,
13.5167516353855));
#155235=CARTESIAN_POINT('Ctrl Pts',(-17.8319662179374,-21.3478161565566,
13.5209247867335));
#155236=CARTESIAN_POINT('Ctrl Pts',(-17.9105916919263,-21.377418942845,
13.5250955297908));
#155237=CARTESIAN_POINT('Ctrl Pts',(-17.9907288118313,-21.4031670920381,
13.5292662728482));
#155238=CARTESIAN_POINT('Ctrl Pts',(-18.0719642714498,-21.4249150195919,
13.5334370159055));
#155239=CARTESIAN_POINT('Ctrl Pts',(-18.1531772197455,-21.4466569205333,
13.5376066031998));
#155240=CARTESIAN_POINT('Ctrl Pts',(-18.2354874590825,-21.4644006827327,
13.541776190494));
#155241=CARTESIAN_POINT('Ctrl Pts',(-18.3184670930211,-21.4780507523044,
13.5459457777883));
#155242=CARTESIAN_POINT('Ctrl Pts',(-18.4014486240669,-21.4917011339484,
13.550115460409));
#155243=CARTESIAN_POINT('Ctrl Pts',(-18.4850991259487,-21.5012575637275,
13.5542851430298));
#155244=CARTESIAN_POINT('Ctrl Pts',(-18.5689824521641,-21.5066759498821,
13.5584548256505));
#155245=CARTESIAN_POINT('Ctrl Pts',(-18.6529508563463,-21.5120998315899,
13.5626287373372));
#155246=CARTESIAN_POINT('Ctrl Pts',(-18.7371520964114,-21.5133772565597,
13.5668026490239));
#155247=CARTESIAN_POINT('Ctrl Pts',(-18.8211473385815,-21.5105162382479,
13.5709765607106));
#155248=CARTESIAN_POINT('Ctrl Pts',(-18.9051840123408,-21.5076538087069,
13.5751525312257));
#155249=CARTESIAN_POINT('Ctrl Pts',(-18.9890140268519,-21.500648907998,
13.5793285017409));
#155250=CARTESIAN_POINT('Ctrl Pts',(-19.0722034479546,-21.4895615121198,
13.583504472256));
#155251=CARTESIAN_POINT('Ctrl Pts',(-19.1555422636085,-21.4784542050977,
13.587687942129));
#155252=CARTESIAN_POINT('Ctrl Pts',(-19.238237733707,-21.4632498369034,
13.5918714120021));
#155253=CARTESIAN_POINT('Ctrl Pts',(-19.3198659781615,-21.4440596011398,
13.5960548818751));
#155254=CARTESIAN_POINT('Ctrl Pts',(-19.3963301748768,-21.4260833972872,
13.5999736928879));
#155255=CARTESIAN_POINT('Ctrl Pts',(-19.4718577384313,-21.4046102735867,
13.6038925039007));
#155256=CARTESIAN_POINT('Ctrl Pts',(-19.546115225231,-21.379770347654,13.6078113149135));
#155257=CARTESIAN_POINT('Ctrl Pts',(-19.6254097949839,-21.353245463438,
13.6119959493065));
#155258=CARTESIAN_POINT('Ctrl Pts',(-19.7035510491553,-21.3227823154618,
13.6161805836996));
#155259=CARTESIAN_POINT('Ctrl Pts',(-19.7801197445754,-21.2885002632162,
13.6203652180926));
#155260=CARTESIAN_POINT('Ctrl Pts',(-19.8565794539351,-21.2542670072287,
13.6245438961766));
#155261=CARTESIAN_POINT('Ctrl Pts',(-19.9314706343179,-21.2162258304372,
13.6287225742605));
#155262=CARTESIAN_POINT('Ctrl Pts',(-20.0043903176931,-21.1745454867587,
13.6329012523444));
#155263=CARTESIAN_POINT('Ctrl Pts',(-20.0786170339864,-21.1321180528749,
13.6371548302299));
#155264=CARTESIAN_POINT('Ctrl Pts',(-20.1508004226817,-21.0859198576824,
13.6414084081153));
#155265=CARTESIAN_POINT('Ctrl Pts',(-20.2205378947047,-21.0361797157652,
13.6456619860008));
#155266=CARTESIAN_POINT('Ctrl Pts',(-20.288923369751,-20.9874038835589,
13.6498330999787));
#155267=CARTESIAN_POINT('Ctrl Pts',(-20.3549565277687,-20.9352224936049,
13.6540042139567));
#155268=CARTESIAN_POINT('Ctrl Pts',(-20.4182851699542,-20.879896124347,
13.6581753279346));
#155269=CARTESIAN_POINT('Ctrl Pts',(-20.4815925616022,-20.8245883203867,
13.662345042255));
#155270=CARTESIAN_POINT('Ctrl Pts',(-20.5421968936247,-20.7661379354359,
13.6665147565753));
#155271=CARTESIAN_POINT('Ctrl Pts',(-20.5997791685762,-20.7048457131497,
13.6706844708957));
#155272=CARTESIAN_POINT('Ctrl Pts',(-20.6573593945033,-20.6435556719038,
13.6748540368398));
#155273=CARTESIAN_POINT('Ctrl Pts',(-20.7119174628063,-20.5794243302492,
13.6790236027838));
#155274=CARTESIAN_POINT('Ctrl Pts',(-20.763172325239,-20.512788158106,13.6831931687278));
#155275=CARTESIAN_POINT('Ctrl Pts',(-20.8162292454053,-20.4438091403549,
13.6875093314668));
#155276=CARTESIAN_POINT('Ctrl Pts',(-20.8657460348867,-20.3721462932499,
13.6918254942057));
#155277=CARTESIAN_POINT('Ctrl Pts',(-20.9114587072171,-20.2982071082729,
13.6961416569446));
#155278=CARTESIAN_POINT('Ctrl Pts',(-20.9556822940544,-20.2266764844696,
13.7003172211363));
#155279=CARTESIAN_POINT('Ctrl Pts',(-20.9963456096573,-20.1530159839384,
13.704492785328));
#155280=CARTESIAN_POINT('Ctrl Pts',(-21.0332565704859,-20.0776194841408,
13.7086683495196));
#155281=CARTESIAN_POINT('Ctrl Pts',(-21.0720318161985,-19.9984148863766,
13.7130548115322));
#155282=CARTESIAN_POINT('Ctrl Pts',(-21.1066654530388,-19.9172948468639,
13.7174412735447));
#155283=CARTESIAN_POINT('Ctrl Pts',(-21.1369928787006,-19.8347373476376,
13.7218277355573));
#155284=CARTESIAN_POINT('Ctrl Pts',(-21.1673203043624,-19.7521798484113,
13.7262141975698));
#155285=CARTESIAN_POINT('Ctrl Pts',(-21.1933414198056,-19.668185466211,
13.7306006595824));
#155286=CARTESIAN_POINT('Ctrl Pts',(-21.214953227824,-19.5832456584798,
13.7349871215949));
#155287=CARTESIAN_POINT('Ctrl Pts',(-21.2416966549182,-19.4781373050501,
13.740415127754));
#155288=CARTESIAN_POINT('Ctrl Pts',(-21.261771847948,-19.3712684537292,
13.7458431339132));
#155289=CARTESIAN_POINT('Ctrl Pts',(-21.2749934581328,-19.2633715557439,
13.7512711400723));
#155290=CARTESIAN_POINT('Ctrl Pts',(-21.2875287526693,-19.1610754377283,
13.7564173858775));
#155291=CARTESIAN_POINT('Ctrl Pts',(-21.2939037306885,-19.05785506064,13.7615636316826));
#155292=CARTESIAN_POINT('Ctrl Pts',(-21.2939989173812,-18.9543543592142,
13.7667098774877));
#155293=CARTESIAN_POINT('Ctrl Pts',(-21.2935815865034,-18.9543537192076,
13.7667098902285));
#155294=CARTESIAN_POINT('Ctrl Pts',(-21.2877697346816,-18.3145386563719,
13.7985275695778));
#155295=CARTESIAN_POINT('Ctrl Pts',(-20.7208249375185,-16.8130884735802,
13.8727371844876));
#155296=CARTESIAN_POINT('Ctrl Pts',(-18.1988330759633,-15.9725894556499,
13.9893387349578));
#155297=CARTESIAN_POINT('Ctrl Pts',(-15.939111528405,-17.7892922724466,
14.1165145416392));
#155298=CARTESIAN_POINT('Ctrl Pts',(-16.1737486300813,-20.0117707719198,
14.2145391051794));
#155299=CARTESIAN_POINT('Ctrl Pts',(-16.9627571743812,-20.8199785653492,
14.2701717331591));
#155300=CARTESIAN_POINT('Ctrl Pts',(-17.1756294737626,-20.9805869941179,
14.2834124255784));
#155301=CARTESIAN_POINT('Origin',(-18.734,-18.952,-1.76670989022851));
#155302=CARTESIAN_POINT('',(-17.1744641402401,-20.9821349467764,15.1499553790579));
#155303=CARTESIAN_POINT('',(-17.1744641402401,-20.9821349467765,15.0832685784559));
#155304=CARTESIAN_POINT('',(-17.1744641402401,-20.9821349467765,-1.76670989022851));
#155305=CARTESIAN_POINT('',(-21.2941233742573,-18.953130183291,14.6332901097715));
#155306=CARTESIAN_POINT('Ctrl Pts',(-21.2939997505486,-18.9531301287165,
14.6332901097715));
#155307=CARTESIAN_POINT('Ctrl Pts',(-21.2940362985033,-18.8703406609988,
14.6374299052976));
#155308=CARTESIAN_POINT('Ctrl Pts',(-21.2900525381051,-18.7873874928942,
14.6415697008237));
#155309=CARTESIAN_POINT('Ctrl Pts',(-21.2820270867845,-18.7046986352398,
14.6457094963498));
#155310=CARTESIAN_POINT('Ctrl Pts',(-21.2740124509524,-18.6221212131097,
14.6498437128863));
#155311=CARTESIAN_POINT('Ctrl Pts',(-21.2619669829652,-18.5398078587026,
14.6539779294227));
#155312=CARTESIAN_POINT('Ctrl Pts',(-21.2459213201025,-18.4581869973214,
14.6581121459591));
#155313=CARTESIAN_POINT('Ctrl Pts',(-21.2298921267196,-18.3766499126674,
14.6622421190812));
#155314=CARTESIAN_POINT('Ctrl Pts',(-21.2098709847548,-18.2958043686398,
14.6663720922033));
#155315=CARTESIAN_POINT('Ctrl Pts',(-21.1859402178852,-18.2160725797221,
14.6705020653254));
#155316=CARTESIAN_POINT('Ctrl Pts',(-21.1620224032905,-18.1363839447932,
14.6746298031432));
#155317=CARTESIAN_POINT('Ctrl Pts',(-21.1341992976673,-18.0578083185522,
14.6787575409609));
#155318=CARTESIAN_POINT('Ctrl Pts',(-21.1026037847562,-17.9807553805356,
14.6828852787787));
#155319=CARTESIAN_POINT('Ctrl Pts',(-21.0710154147149,-17.9037198620526,
14.6870120834293));
#155320=CARTESIAN_POINT('Ctrl Pts',(-21.0356565094079,-17.8282067834225,
14.69113888808));
#155321=CARTESIAN_POINT('Ctrl Pts',(-20.9967085276618,-17.7546069488901,
14.6952656927306));
#155322=CARTESIAN_POINT('Ctrl Pts',(-20.9577570758465,-17.6810005569824,
14.6993928650588));
#155323=CARTESIAN_POINT('Ctrl Pts',(-20.9152161348637,-17.6093081624228,
14.703520037387));
#155324=CARTESIAN_POINT('Ctrl Pts',(-20.8693129406038,-17.5398956675621,
14.7076472097152));
#155325=CARTESIAN_POINT('Ctrl Pts',(-20.8233622278895,-17.4704113176916,
14.7117786544444));
#155326=CARTESIAN_POINT('Ctrl Pts',(-20.7740425759674,-17.4032119705945,
14.7159100991735));
#155327=CARTESIAN_POINT('Ctrl Pts',(-20.7216239583869,-17.3386336435743,
14.7200415439027));
#155328=CARTESIAN_POINT('Ctrl Pts',(-20.6691749218115,-17.2740178411706,
14.7241753861463));
#155329=CARTESIAN_POINT('Ctrl Pts',(-20.6136236562292,-17.2120264344647,
14.7283092283899));
#155330=CARTESIAN_POINT('Ctrl Pts',(-20.5552780488236,-17.1529596255578,
14.7324430706336));
#155331=CARTESIAN_POINT('Ctrl Pts',(-20.4968364594113,-17.0937956482246,
14.7365837132944));
#155332=CARTESIAN_POINT('Ctrl Pts',(-20.4355917013472,-17.0375661867587,
14.7407243559553));
#155333=CARTESIAN_POINT('Ctrl Pts',(-20.3718854170603,-16.9845317383548,
14.7448649986162));
#155334=CARTESIAN_POINT('Ctrl Pts',(-20.3405294527256,-16.9584284066148,
14.7469030054636));
#155335=CARTESIAN_POINT('Ctrl Pts',(-20.3085776248464,-16.9330984310457,
14.7489410123109));
#155336=CARTESIAN_POINT('Ctrl Pts',(-20.2760730898183,-16.9085689182999,
14.7509790191583));
#155337=CARTESIAN_POINT('Ctrl Pts',(-20.2093316088542,-16.8582025307612,
14.7551636535514));
#155338=CARTESIAN_POINT('Ctrl Pts',(-20.1399957688999,-16.811015665153,
14.7593482879444));
#155339=CARTESIAN_POINT('Ctrl Pts',(-20.0684012262925,-16.767286433587,
14.7635329223375));
#155340=CARTESIAN_POINT('Ctrl Pts',(-19.9969085896549,-16.7236194451695,
14.7677116004214));
#155341=CARTESIAN_POINT('Ctrl Pts',(-19.9231640255692,-16.6834005528598,
14.7718902785053));
#155342=CARTESIAN_POINT('Ctrl Pts',(-19.8475347050067,-16.6468664982814,
14.7760689565893));
#155343=CARTESIAN_POINT('Ctrl Pts',(-19.7705497832269,-16.6096775970311,
14.7803225344747));
#155344=CARTESIAN_POINT('Ctrl Pts',(-19.6916122567006,-16.5763072247155,
14.7845761123601));
#155345=CARTESIAN_POINT('Ctrl Pts',(-19.6111386006651,-16.5469578225688,
14.7888296902456));
#155346=CARTESIAN_POINT('Ctrl Pts',(-19.5322250834833,-16.5181774158532,
14.7930008042235));
#155347=CARTESIAN_POINT('Ctrl Pts',(-19.4518349191003,-16.4932636267838,
14.7971719182015));
#155348=CARTESIAN_POINT('Ctrl Pts',(-19.3703822558338,-16.4723593759458,
14.8013430321794));
#155349=CARTESIAN_POINT('Ctrl Pts',(-19.288956924795,-16.4514621397311,
14.8055127464998));
#155350=CARTESIAN_POINT('Ctrl Pts',(-19.2064702481718,-16.4345718839471,
14.8096824608202));
#155351=CARTESIAN_POINT('Ctrl Pts',(-19.1233507011893,-16.4217814261445,
14.8138521751405));
#155352=CARTESIAN_POINT('Ctrl Pts',(-19.040234111957,-16.4089914234813,
14.8180217410846));
#155353=CARTESIAN_POINT('Ctrl Pts',(-18.9564851519522,-16.4003009978601,
14.8221913070286));
#155354=CARTESIAN_POINT('Ctrl Pts',(-18.8725402767199,-16.3957514612764,
14.8263608729727));
#155355=CARTESIAN_POINT('Ctrl Pts',(-18.7856440032318,-16.3910419685989,
14.8306770357116));
#155356=CARTESIAN_POINT('Ctrl Pts',(-18.6985383080788,-16.3907699986349,
14.8349931984505));
#155357=CARTESIAN_POINT('Ctrl Pts',(-18.6117085473889,-16.3949226056652,
14.8393093611894));
#155358=CARTESIAN_POINT('Ctrl Pts',(-18.5277072570205,-16.3989399419582,
14.8434849253811));
#155359=CARTESIAN_POINT('Ctrl Pts',(-18.4439646643006,-16.4070979281598,
14.8476604895728));
#155360=CARTESIAN_POINT('Ctrl Pts',(-18.3609142114861,-16.4193320402372,
14.8518360537644));
#155361=CARTESIAN_POINT('Ctrl Pts',(-18.2736690777338,-16.4321840682319,
14.856222515777));
#155362=CARTESIAN_POINT('Ctrl Pts',(-18.1871884138653,-16.4495346990029,
14.8606089777895));
#155363=CARTESIAN_POINT('Ctrl Pts',(-18.1019594530764,-16.471249156597,
14.864995439802));
#155364=CARTESIAN_POINT('Ctrl Pts',(-18.0167304922876,-16.4929636141912,
14.8693819018146));
#155365=CARTESIAN_POINT('Ctrl Pts',(-17.932753766134,-16.5190416538915,
14.8737683638271));
#155366=CARTESIAN_POINT('Ctrl Pts',(-17.8504927560606,-16.549290082031,
14.8781548258397));
#155367=CARTESIAN_POINT('Ctrl Pts',(-17.7720166970007,-16.5781467351529,
14.8823394602327));
#155368=CARTESIAN_POINT('Ctrl Pts',(-17.6948098353985,-16.6109058485358,
14.8865240946257));
#155369=CARTESIAN_POINT('Ctrl Pts',(-17.6192877039368,-16.6474357251303,
14.8907087290188));
#155370=CARTESIAN_POINT('Ctrl Pts',(-17.5438730688816,-16.683913605967,
14.8948874071027));
#155371=CARTESIAN_POINT('Ctrl Pts',(-17.4701388113635,-16.7241513904372,
14.8990660851867));
#155372=CARTESIAN_POINT('Ctrl Pts',(-17.3984827363055,-16.7679684896106,
14.9032447632706));
#155373=CARTESIAN_POINT('Ctrl Pts',(-17.3255422776003,-16.8125709787959,
14.9074983411561));
#155374=CARTESIAN_POINT('Ctrl Pts',(-17.2547556895186,-16.8608821968549,
14.9117519190415));
#155375=CARTESIAN_POINT('Ctrl Pts',(-17.1865186232482,-16.912661531622,
14.9160054969269));
#155376=CARTESIAN_POINT('Ctrl Pts',(-17.1196044656613,-16.9634370229455,
14.9201766109049));
#155377=CARTESIAN_POINT('Ctrl Pts',(-17.0551422404859,-17.0175470676763,
14.9243477248828));
#155378=CARTESIAN_POINT('Ctrl Pts',(-16.9934762919463,-17.0747207928219,
14.9285188388608));
#155379=CARTESIAN_POINT('Ctrl Pts',(-16.9318310360114,-17.1318753327718,
14.9326885531811));
#155380=CARTESIAN_POINT('Ctrl Pts',(-16.8729805302655,-17.1920911989054,
14.9368582675015));
#155381=CARTESIAN_POINT('Ctrl Pts',(-16.8172347450926,-17.2550583517457,
14.9410279818219));
#155382=CARTESIAN_POINT('Ctrl Pts',(-16.7614909435939,-17.3180232639448,
14.9451975477659));
#155383=CARTESIAN_POINT('Ctrl Pts',(-16.70885194731,-17.383738923187,14.94936711371));
#155384=CARTESIAN_POINT('Ctrl Pts',(-16.6595887382,-17.451860700829,14.953536679654));
#155385=CARTESIAN_POINT('Ctrl Pts',(-16.6085934954305,-17.5223775561355,
14.957852842393));
#155386=CARTESIAN_POINT('Ctrl Pts',(-16.5612161510347,-17.5954724488009,
14.9621690051319));
#155387=CARTESIAN_POINT('Ctrl Pts',(-16.517708533778,-17.6707302638587,
14.9664851678708));
#155388=CARTESIAN_POINT('Ctrl Pts',(-16.4756181725772,-17.7435365635068,
14.9706607320625));
#155389=CARTESIAN_POINT('Ctrl Pts',(-16.437149470808,-17.8183665946342,
14.9748362962542));
#155390=CARTESIAN_POINT('Ctrl Pts',(-16.4024827880428,-17.8948209752613,
14.9790118604458));
#155391=CARTESIAN_POINT('Ctrl Pts',(-16.3660651735434,-17.9751368849009,
14.9833983224584));
#155392=CARTESIAN_POINT('Ctrl Pts',(-16.3338439651084,-18.0572450047083,
14.9877847844709));
#155393=CARTESIAN_POINT('Ctrl Pts',(-16.3059695675778,-18.1406626970049,
14.9921712464835));
#155394=CARTESIAN_POINT('Ctrl Pts',(-16.2780951700471,-18.2240803893014,
14.996557708496));
#155395=CARTESIAN_POINT('Ctrl Pts',(-16.2545676653734,-18.3088070746724,
15.0009441705086));
#155396=CARTESIAN_POINT('Ctrl Pts',(-16.2354754819719,-18.3943484665023,
15.0053306325211));
#155397=CARTESIAN_POINT('Ctrl Pts',(-16.21726175823,-18.4759539720914,15.0095152669141));
#155398=CARTESIAN_POINT('Ctrl Pts',(-16.2030163785017,-18.5586046111966,
15.0136999013072));
#155399=CARTESIAN_POINT('Ctrl Pts',(-16.1928535263697,-18.6418797014763,
15.0178845357003));
#155400=CARTESIAN_POINT('Ctrl Pts',(-16.1827051397999,-18.7250362599721,
15.0220632137842));
#155401=CARTESIAN_POINT('Ctrl Pts',(-16.1766277936582,-18.8088150514092,
15.0262418918681));
#155402=CARTESIAN_POINT('Ctrl Pts',(-16.1746849654928,-18.8927838354387,
15.0304205699521));
#155403=CARTESIAN_POINT('Ctrl Pts',(-16.1727073135288,-18.9782576995748,
15.0346741478375));
#155404=CARTESIAN_POINT('Ctrl Pts',(-16.1750139649456,-19.0639279639716,
15.0389277257229));
#155405=CARTESIAN_POINT('Ctrl Pts',(-16.1816167614736,-19.1493317097918,
15.0431813036084));
#155406=CARTESIAN_POINT('Ctrl Pts',(-16.1880915499065,-19.2330797373476,
15.0473524175863));
#155407=CARTESIAN_POINT('Ctrl Pts',(-16.1986973545603,-19.3165710082865,
15.0515235315643));
#155408=CARTESIAN_POINT('Ctrl Pts',(-16.2133928011124,-19.3993693651963,
15.0556946455422));
#155409=CARTESIAN_POINT('Ctrl Pts',(-16.2280833164655,-19.4821399383178,
15.0598643598626));
#155410=CARTESIAN_POINT('Ctrl Pts',(-16.2468606679443,-19.5642176066097,
15.064034074183));
#155411=CARTESIAN_POINT('Ctrl Pts',(-16.2696319425036,-19.6451739155444,
15.0682037885034));
#155412=CARTESIAN_POINT('Ctrl Pts',(-16.2924024067631,-19.7261273437062,
15.0723733544474));
#155413=CARTESIAN_POINT('Ctrl Pts',(-16.3191663861463,-19.8059590492308,
15.0765429203914));
#155414=CARTESIAN_POINT('Ctrl Pts',(-16.3497807798976,-19.8842546382262,
15.0807124863355));
#155415=CARTESIAN_POINT('Ctrl Pts',(-16.3814715379662,-19.9653030035426,
15.0850286490744));
#155416=CARTESIAN_POINT('Ctrl Pts',(-16.4172883172412,-20.0447047315975,
15.0893448118133));
#155417=CARTESIAN_POINT('Ctrl Pts',(-16.4570183818636,-20.1220233803941,
15.0936609745523));
#155418=CARTESIAN_POINT('Ctrl Pts',(-16.4954542438098,-20.1968233823387,
15.0978365387439));
#155419=CARTESIAN_POINT('Ctrl Pts',(-16.5375520792277,-20.2696735493081,
15.1020121029356));
#155420=CARTESIAN_POINT('Ctrl Pts',(-16.583073696292,-20.3402060495535,
15.1061876671273));
#155421=CARTESIAN_POINT('Ctrl Pts',(-16.6308945020168,-20.4143009787112,
15.1105741291398));
#155422=CARTESIAN_POINT('Ctrl Pts',(-16.6824937078808,-20.4858374838362,
15.1149605911524));
#155423=CARTESIAN_POINT('Ctrl Pts',(-16.7375469032625,-20.5544278556389,
15.1193470531649));
#155424=CARTESIAN_POINT('Ctrl Pts',(-16.7926000986442,-20.6230182274415,
15.1237335151774));
#155425=CARTESIAN_POINT('Ctrl Pts',(-16.8511068407071,-20.6886620833861,
15.12811997719));
#155426=CARTESIAN_POINT('Ctrl Pts',(-16.9126993772538,-20.7510175211999,
15.1325064392025));
#155427=CARTESIAN_POINT('Ctrl Pts',(-16.9714542743191,-20.8105001717875,
15.1366908118307));
#155428=CARTESIAN_POINT('Ctrl Pts',(-17.0332355735422,-20.8672121310249,
15.1408751844589));
#155429=CARTESIAN_POINT('Ctrl Pts',(-17.0977514090968,-20.9208297409291,
15.1450595570871));
#155430=CARTESIAN_POINT('Ctrl Pts',(-17.1229131297205,-20.9417410615271,
15.146691497744));
#155431=CARTESIAN_POINT('Ctrl Pts',(-17.1484903532052,-20.9621820602163,
15.1483234384009));
#155432=CARTESIAN_POINT('Ctrl Pts',(-17.1744641402401,-20.9821349467764,
15.1499553790579));
#155433=CARTESIAN_POINT('Ctrl Pts',(-17.1732300411181,-20.9837128798172,
14.34978651614));
#155434=CARTESIAN_POINT('Ctrl Pts',(-17.2767521098951,-21.0647994924116,
14.356341543798));
#155435=CARTESIAN_POINT('Ctrl Pts',(-18.0960849332152,-21.6081172949695,
14.4052885070165));
#155436=CARTESIAN_POINT('Ctrl Pts',(-20.1784866529944,-21.6122160192327,
14.4966274057954));
#155437=CARTESIAN_POINT('Ctrl Pts',(-21.2671017221445,-19.9284206152422,
14.5845735760146));
#155438=CARTESIAN_POINT('Ctrl Pts',(-21.2979708163172,-19.0164624131716,
14.6301278106733));
#155439=CARTESIAN_POINT('Ctrl Pts',(-21.2976210374783,-18.9531317273574,
14.6332901097715));
#155440=CARTESIAN_POINT('',(-21.2936354977614,-18.9514398261094,14.566709915054));
#155441=CARTESIAN_POINT('Ctrl Pts',(-17.1756294737626,-20.9805869941179,
14.2834124255784));
#155442=CARTESIAN_POINT('Ctrl Pts',(-17.6442977246966,-21.3341889968917,
14.3125636687196));
#155443=CARTESIAN_POINT('Ctrl Pts',(-19.0929371519294,-21.824338083774,
14.3841068474214));
#155444=CARTESIAN_POINT('Ctrl Pts',(-20.9482575115022,-20.7321304478324,
14.478539335638));
#155445=CARTESIAN_POINT('Ctrl Pts',(-21.2889974874197,-19.4133916920799,
14.5438205807135));
#155446=CARTESIAN_POINT('Ctrl Pts',(-21.2898969963344,-18.9514411453738,
14.5667098902285));
#155447=CARTESIAN_POINT('Ctrl Pts',(-21.2939999386838,-18.9514396975034,
14.566709917474));
#155448=CARTESIAN_POINT('Ctrl Pts',(-21.2939802627005,-18.8615409084184,
14.571157199273));
#155449=CARTESIAN_POINT('Ctrl Pts',(-21.2892209204008,-18.7717655181781,
14.575604481072));
#155450=CARTESIAN_POINT('Ctrl Pts',(-21.2797861099468,-18.6826060832129,
14.5800517628709));
#155451=CARTESIAN_POINT('Ctrl Pts',(-21.2703167670437,-18.5931203148612,
14.5845153222128));
#155452=CARTESIAN_POINT('Ctrl Pts',(-21.2561377674616,-18.5042553694628,
14.5889788815547));
#155453=CARTESIAN_POINT('Ctrl Pts',(-21.2373647797459,-18.4164957707656,
14.5934424408966));
#155454=CARTESIAN_POINT('Ctrl Pts',(-21.2185553401018,-18.3285657673013,
14.5979146672311));
#155455=CARTESIAN_POINT('Ctrl Pts',(-21.1951342035189,-18.2417457397356,
14.6023868935656));
#155456=CARTESIAN_POINT('Ctrl Pts',(-21.1672666877164,-18.1565044145631,
14.6068591199));
#155457=CARTESIAN_POINT('Ctrl Pts',(-21.139316159677,-18.0710091710603,
14.6113446681795));
#155458=CARTESIAN_POINT('Ctrl Pts',(-21.1068928974786,-17.9871023685111,
14.6158302164589));
#155459=CARTESIAN_POINT('Ctrl Pts',(-21.0702104967804,-17.9052333045357,
14.6203157647383));
#155460=CARTESIAN_POINT('Ctrl Pts',(-21.0568477853901,-17.875409938211,
14.6219497659472));
#155461=CARTESIAN_POINT('Ctrl Pts',(-21.0429203172351,-17.8458567318452,
14.6235837671561));
#155462=CARTESIAN_POINT('Ctrl Pts',(-21.0284398795323,-17.8165945044999,
14.625217768365));
#155463=CARTESIAN_POINT('Ctrl Pts',(-20.9913558570061,-17.7416547050056,
14.629402402758));
#155464=CARTESIAN_POINT('Ctrl Pts',(-20.9505274948144,-17.6683941847451,
14.6335870371511));
#155465=CARTESIAN_POINT('Ctrl Pts',(-20.9061301751471,-17.5972120083883,
14.6377716715441));
#155466=CARTESIAN_POINT('Ctrl Pts',(-20.8617960495691,-17.526131151049,
14.641950349628));
#155467=CARTESIAN_POINT('Ctrl Pts',(-20.8139032983065,-17.4571231485616,
14.646129027712));
#155468=CARTESIAN_POINT('Ctrl Pts',(-20.7626740190629,-17.3905642106128,
14.6503077057959));
#155469=CARTESIAN_POINT('Ctrl Pts',(-20.7105264918066,-17.3228122515362,
14.6545612836814));
#155470=CARTESIAN_POINT('Ctrl Pts',(-20.6549218593555,-17.2575984516732,
14.6588148615668));
#155471=CARTESIAN_POINT('Ctrl Pts',(-20.5961416680529,-17.1952904599504,
14.6630684394522));
#155472=CARTESIAN_POINT('Ctrl Pts',(-20.5385010454588,-17.1341904302312,
14.6672395534302));
#155473=CARTESIAN_POINT('Ctrl Pts',(-20.4778072242623,-17.0758848946115,
14.6714106674082));
#155474=CARTESIAN_POINT('Ctrl Pts',(-20.4143663508876,-17.0206872529792,
14.6755817813861));
#155475=CARTESIAN_POINT('Ctrl Pts',(-20.3509467657105,-16.9655081334487,
14.6797514957065));
#155476=CARTESIAN_POINT('Ctrl Pts',(-20.2847823058332,-16.9134351384329,
14.6839212100269));
#155477=CARTESIAN_POINT('Ctrl Pts',(-20.2162143833074,-16.8647433023423,
14.6880909243472));
#155478=CARTESIAN_POINT('Ctrl Pts',(-20.1476489007225,-16.8160531989163,
14.6922604902913));
#155479=CARTESIAN_POINT('Ctrl Pts',(-20.0766805011101,-16.7707442808557,
14.6964300562353));
#155480=CARTESIAN_POINT('Ctrl Pts',(-20.0036808175632,-16.7290491185112,
14.7005996221793));
#155481=CARTESIAN_POINT('Ctrl Pts',(-19.9281145551976,-16.6858880056951,
14.7049157849183));
#155482=CARTESIAN_POINT('Ctrl Pts',(-19.8503719693232,-16.6465997576134,
14.7092319476572));
#155483=CARTESIAN_POINT('Ctrl Pts',(-19.7708927266888,-16.6113903628884,
14.7135481103961));
#155484=CARTESIAN_POINT('Ctrl Pts',(-19.6940025120236,-16.5773279104931,
14.7177236745878));
#155485=CARTESIAN_POINT('Ctrl Pts',(-19.6154875027975,-16.5470827802972,
14.7218992387795));
#155486=CARTESIAN_POINT('Ctrl Pts',(-19.5357640795054,-16.5207915842498,
14.7260748029711));
#155487=CARTESIAN_POINT('Ctrl Pts',(-19.4520140156272,-16.4931724823913,
14.7304612649837));
#155488=CARTESIAN_POINT('Ctrl Pts',(-19.3669308187545,-16.4699173921691,
14.7348477269962));
#155489=CARTESIAN_POINT('Ctrl Pts',(-19.2810104439707,-16.4511242385542,
14.7392341890088));
#155490=CARTESIAN_POINT('Ctrl Pts',(-19.1950900691869,-16.4323310849393,
14.7436206510213));
#155491=CARTESIAN_POINT('Ctrl Pts',(-19.1083331013483,-16.4179998874471,
14.7480071130339));
#155492=CARTESIAN_POINT('Ctrl Pts',(-19.021240449396,-16.4081657042506,
14.7523935750464));
#155493=CARTESIAN_POINT('Ctrl Pts',(-18.9381550594622,-16.3987840064008,
14.7565782094394));
#155494=CARTESIAN_POINT('Ctrl Pts',(-18.8544549375686,-16.3934596676543,
14.7607628438325));
#155495=CARTESIAN_POINT('Ctrl Pts',(-18.770570565002,-16.3922612254811,
14.7649474782255));
#155496=CARTESIAN_POINT('Ctrl Pts',(-18.6868055914571,-16.3910644891421,
14.7691261563095));
#155497=CARTESIAN_POINT('Ctrl Pts',(-18.6028573442178,-16.3939819908556,
14.7733048343934));
#155498=CARTESIAN_POINT('Ctrl Pts',(-18.5191623733687,-16.4010306167687,
14.7774835124774));
#155499=CARTESIAN_POINT('Ctrl Pts',(-18.4339672303176,-16.4082055842356,
14.7817370903628));
#155500=CARTESIAN_POINT('Ctrl Pts',(-18.3490350120199,-16.4196612875147,
14.7859906682482));
#155501=CARTESIAN_POINT('Ctrl Pts',(-18.2648272487369,-16.4353599920783,
14.7902442461337));
#155502=CARTESIAN_POINT('Ctrl Pts',(-18.182252017263,-16.4507543466204,
14.7944153601116));
#155503=CARTESIAN_POINT('Ctrl Pts',(-18.1003738745937,-16.4702285646622,
14.7985864740896));
#155504=CARTESIAN_POINT('Ctrl Pts',(-18.0196220516907,-16.493694862925,
14.8027575880675));
#155505=CARTESIAN_POINT('Ctrl Pts',(-17.9388973258418,-16.5171532868448,
14.8069273023879));
#155506=CARTESIAN_POINT('Ctrl Pts',(-17.8592986105402,-16.5446010022893,
14.8110970167083));
#155507=CARTESIAN_POINT('Ctrl Pts',(-17.7812419660685,-16.5758998066624,
14.8152667310286));
#155508=CARTESIAN_POINT('Ctrl Pts',(-17.7031880991871,-16.6071974972898,
14.8194362969727));
#155509=CARTESIAN_POINT('Ctrl Pts',(-17.6266766207018,-16.6423458323765,
14.8236058629167));
#155510=CARTESIAN_POINT('Ctrl Pts',(-17.552104243417,-16.6811582132233,
14.8277754288608));
#155511=CARTESIAN_POINT('Ctrl Pts',(-17.4749099933419,-16.7213351895004,
14.8320915915997));
#155512=CARTESIAN_POINT('Ctrl Pts',(-17.3997942069763,-16.7654384176638,
14.8364077543386));
#155513=CARTESIAN_POINT('Ctrl Pts',(-17.3271680714252,-16.8132097052907,
14.8407239170775));
#155514=CARTESIAN_POINT('Ctrl Pts',(-17.2569077246007,-16.8594248482479,
14.8448994812692));
#155515=CARTESIAN_POINT('Ctrl Pts',(-17.1889776711625,-16.9090724304067,
14.8490750454609));
#155516=CARTESIAN_POINT('Ctrl Pts',(-17.1237181590048,-16.9618762871215,
14.8532506096526));
#155517=CARTESIAN_POINT('Ctrl Pts',(-17.0551625440278,-17.0173471411098,
14.8576370716651));
#155518=CARTESIAN_POINT('Ctrl Pts',(-16.9895547726121,-17.0763011057024,
14.8620235336777));
#155519=CARTESIAN_POINT('Ctrl Pts',(-16.9272456352414,-17.13837416609,14.8664099956902));
#155520=CARTESIAN_POINT('Ctrl Pts',(-16.8649364978707,-17.2004472264777,
14.8707964577027));
#155521=CARTESIAN_POINT('Ctrl Pts',(-16.8059263275258,-17.2656389014522,
14.8751829197153));
#155522=CARTESIAN_POINT('Ctrl Pts',(-16.7505157350919,-17.3335469821889,
14.8795693817278));
#155523=CARTESIAN_POINT('Ctrl Pts',(-16.6976546661539,-17.398330511467,
14.8837540161209));
#155524=CARTESIAN_POINT('Ctrl Pts',(-16.6478724513803,-17.4658271045687,
14.8879386505139));
#155525=CARTESIAN_POINT('Ctrl Pts',(-16.6014597312929,-17.5357118928894,
14.892123284907));
#155526=CARTESIAN_POINT('Ctrl Pts',(-16.5551130739679,-17.605497208864,
14.8963019629909));
#155527=CARTESIAN_POINT('Ctrl Pts',(-16.5121266371781,-17.6776635880369,
14.9004806410749));
#155528=CARTESIAN_POINT('Ctrl Pts',(-16.4727509157818,-17.7518531010238,
14.9046593191588));
#155529=CARTESIAN_POINT('Ctrl Pts',(-16.4326694128783,-17.8273724077119,
14.9089128970443));
#155530=CARTESIAN_POINT('Ctrl Pts',(-16.3963296475342,-17.9049877173956,
14.9131664749297));
#155531=CARTESIAN_POINT('Ctrl Pts',(-16.3639497085597,-17.98429053118,14.9174200528151));
#155532=CARTESIAN_POINT('Ctrl Pts',(-16.3321975178866,-18.0620559051724,
14.9215911667931));
#155533=CARTESIAN_POINT('Ctrl Pts',(-16.3042531677127,-18.1414434905287,
14.925762280771));
#155534=CARTESIAN_POINT('Ctrl Pts',(-16.2802751807717,-18.2220448565132,
14.929933394749));
#155535=CARTESIAN_POINT('Ctrl Pts',(-16.2563052398757,-18.302619175931,
14.9341031090694));
#155536=CARTESIAN_POINT('Ctrl Pts',(-16.2362991499856,-18.3844060265128,
14.9382728233897));
#155537=CARTESIAN_POINT('Ctrl Pts',(-16.2203659101291,-18.4669807609602,
14.9424425377101));
#155538=CARTESIAN_POINT('Ctrl Pts',(-16.2044332372455,-18.5495525570442,
14.9466121036542));
#155539=CARTESIAN_POINT('Ctrl Pts',(-16.1925732125598,-18.6329117293879,
14.9507816695982));
#155540=CARTESIAN_POINT('Ctrl Pts',(-16.1848436692123,-18.7166237029672,
14.9549512355423));
#155541=CARTESIAN_POINT('Ctrl Pts',(-16.1768423646561,-18.8032788862675,
14.9592673982812));
#155542=CARTESIAN_POINT('Ctrl Pts',(-16.1732674495782,-18.890311616191,
14.9635835610201));
#155543=CARTESIAN_POINT('Ctrl Pts',(-16.1741243927921,-18.9772363947927,
14.967899723759));
#155544=CARTESIAN_POINT('Ctrl Pts',(-16.174953421171,-19.0613296078744,
14.9720752879507));
#155545=CARTESIAN_POINT('Ctrl Pts',(-16.1799299313356,-19.1453213272336,
14.9762508521424));
#155546=CARTESIAN_POINT('Ctrl Pts',(-16.1890058822549,-19.228775975552,
14.9804264163341));
#155547=CARTESIAN_POINT('Ctrl Pts',(-16.1985402378791,-19.3164457197621,
14.9848128783466));
#155548=CARTESIAN_POINT('Ctrl Pts',(-16.2125989501167,-19.4035221357512,
14.9891993403591));
#155549=CARTESIAN_POINT('Ctrl Pts',(-16.2310658163555,-19.4895132299243,
14.9935858023717));
#155550=CARTESIAN_POINT('Ctrl Pts',(-16.2495326825942,-19.5755043240973,
14.9979722643842));
#155551=CARTESIAN_POINT('Ctrl Pts',(-16.2724074784503,-19.660409556001,
15.0023587263968));
#155552=CARTESIAN_POINT('Ctrl Pts',(-16.2995147249235,-19.7437584514457,
15.0067451884093));
#155553=CARTESIAN_POINT('Ctrl Pts',(-16.325371504027,-19.8232624313191,
15.0109293012964));
#155554=CARTESIAN_POINT('Ctrl Pts',(-16.3551750808466,-19.9016463915223,
15.0151134141836));
#155555=CARTESIAN_POINT('Ctrl Pts',(-16.3888096569738,-19.9784902605368,
15.0192975270708));
#155556=CARTESIAN_POINT('Ctrl Pts',(-16.422398948156,-20.0552306684471,
15.023476006549));
#155557=CARTESIAN_POINT('Ctrl Pts',(-16.4598088143048,-20.1304346847381,
15.0276544860272));
#155558=CARTESIAN_POINT('Ctrl Pts',(-16.5008739124384,-20.2036979975424,
15.0318329655054));
#155559=CARTESIAN_POINT('Ctrl Pts',(-16.5429986555096,-20.2788517989138,
15.0361192665846));
#155560=CARTESIAN_POINT('Ctrl Pts',(-16.5889697394115,-20.3519628838743,
15.0404055676638));
#155561=CARTESIAN_POINT('Ctrl Pts',(-16.63855629866,-20.4226174534917,15.044691868743));
#155562=CARTESIAN_POINT('Ctrl Pts',(-16.6868081648856,-20.4913702545144,
15.0488627979103));
#155563=CARTESIAN_POINT('Ctrl Pts',(-16.7384830491083,-20.5577967113089,
15.0530337270777));
#155564=CARTESIAN_POINT('Ctrl Pts',(-16.7933230379798,-20.6215427305356,
15.057204656245));
#155565=CARTESIAN_POINT('Ctrl Pts',(-16.8504384170978,-20.6879336640552,
15.0615486432802));
#155566=CARTESIAN_POINT('Ctrl Pts',(-16.9109869827439,-20.7514164472448,
15.0658926303153));
#155567=CARTESIAN_POINT('Ctrl Pts',(-16.974630487842,-20.8116287047927,
15.0702366173505));
#155568=CARTESIAN_POINT('Ctrl Pts',(-17.03827399294,-20.8718409623405,15.0745806043856));
#155569=CARTESIAN_POINT('Ctrl Pts',(-17.1050120275129,-20.9287823061029,
15.0789245914208));
#155570=CARTESIAN_POINT('Ctrl Pts',(-17.1744641402401,-20.9821349467765,
15.0832685784559));
#155571=CARTESIAN_POINT('Origin',(-18.734,-18.952,-1.76670989022851));
#155572=CARTESIAN_POINT('',(-17.1744641402401,-20.9821349467765,15.9499155181261));
#155573=CARTESIAN_POINT('',(-17.172599330006,-20.9845253206546,15.883228700071));
#155574=CARTESIAN_POINT('',(-17.1744641402401,-20.9821349467765,-1.76670989022851));
#155575=CARTESIAN_POINT('',(-21.293999428374,-18.9537107672548,15.4332901097416));
#155576=CARTESIAN_POINT('Ctrl Pts',(-21.2939994283744,-18.9537107666516,
15.4332901097715));
#155577=CARTESIAN_POINT('Ctrl Pts',(-21.2940559692553,-18.8691027211111,
15.437482057942));
#155578=CARTESIAN_POINT('Ctrl Pts',(-21.2899137324165,-18.7844696898645,
15.4416740061124));
#155579=CARTESIAN_POINT('Ctrl Pts',(-21.2815918669692,-18.7002547332074,
15.4458659542829));
#155580=CARTESIAN_POINT('Ctrl Pts',(-21.2732695913204,-18.6160356254257,
15.4500581090829));
#155581=CARTESIAN_POINT('Ctrl Pts',(-21.2607673227297,-18.5322350838833,
15.4542502638829));
#155582=CARTESIAN_POINT('Ctrl Pts',(-21.2441560631151,-18.449290800953,
15.4584424186829));
#155583=CARTESIAN_POINT('Ctrl Pts',(-21.2275392030056,-18.3663185533138,
15.4626359868701));
#155584=CARTESIAN_POINT('Ctrl Pts',(-21.2068106889621,-18.2842035816671,
15.4668295550574));
#155585=CARTESIAN_POINT('Ctrl Pts',(-21.1820923104735,-18.2033718951306,
15.4710231232446));
#155586=CARTESIAN_POINT('Ctrl Pts',(-21.1573415752886,-18.1224343988081,
15.4752221808701));
#155587=CARTESIAN_POINT('Ctrl Pts',(-21.1285906849035,-18.0427839738201,
15.4794212384956));
#155588=CARTESIAN_POINT('Ctrl Pts',(-21.0960107310926,-17.9648296468171,
15.483620296121));
#155589=CARTESIAN_POINT('Ctrl Pts',(-21.0634063961442,-17.8868169828631,
15.4878224961022));
#155590=CARTESIAN_POINT('Ctrl Pts',(-21.0269674888688,-17.8105033515339,
15.4920246960833));
#155591=CARTESIAN_POINT('Ctrl Pts',(-20.9869114421218,-17.7362738655615,
15.4962268960644));
#155592=CARTESIAN_POINT('Ctrl Pts',(-20.9467843119657,-17.6619126520388,
15.5004365532642));
#155593=CARTESIAN_POINT('Ctrl Pts',(-20.9030274638811,-17.5896433529156,
15.5046462104641));
#155594=CARTESIAN_POINT('Ctrl Pts',(-20.8559018807132,-17.5198224940232,
15.5088558676639));
#155595=CARTESIAN_POINT('Ctrl Pts',(-20.8365799691019,-17.4911953158865,
15.5105818648582));
#155596=CARTESIAN_POINT('Ctrl Pts',(-20.8166922183615,-17.4629793510679,
15.5123078620525));
#155597=CARTESIAN_POINT('Ctrl Pts',(-20.7962584977301,-17.435197478727,
15.5140338592469));
#155598=CARTESIAN_POINT('Ctrl Pts',(-20.7467174843303,-17.3678410665132,
15.5182184936399));
#155599=CARTESIAN_POINT('Ctrl Pts',(-20.6937808669812,-17.3027889832896,
15.522403128033));
#155600=CARTESIAN_POINT('Ctrl Pts',(-20.6376906991394,-17.2404037502932,
15.526587762426));
#155601=CARTESIAN_POINT('Ctrl Pts',(-20.581680368709,-17.1781073149544,
15.53076644051));
#155602=CARTESIAN_POINT('Ctrl Pts',(-20.522525708678,-17.1184705290968,
15.5349451185939));
#155603=CARTESIAN_POINT('Ctrl Pts',(-20.4605108062944,-17.061825289623,
15.5391237966778));
#155604=CARTESIAN_POINT('Ctrl Pts',(-20.3973843313549,-17.0041647249419,
15.5433773745633));
#155605=CARTESIAN_POINT('Ctrl Pts',(-20.3312943514667,-16.9496043968549,
15.5476309524487));
#155606=CARTESIAN_POINT('Ctrl Pts',(-20.2625820107878,-16.8984574422973,
15.5518845303342));
#155607=CARTESIAN_POINT('Ctrl Pts',(-20.195201792914,-16.8483020712589,
15.5560556443121));
#155608=CARTESIAN_POINT('Ctrl Pts',(-20.1253003720614,-16.8014291923403,
15.5602267582901));
#155609=CARTESIAN_POINT('Ctrl Pts',(-20.0532336923064,-16.7580942442567,
15.564397872268));
#155610=CARTESIAN_POINT('Ctrl Pts',(-19.9811911952218,-16.7147738376335,
15.5685675865884));
#155611=CARTESIAN_POINT('Ctrl Pts',(-19.9069852761389,-16.6749892409427,
15.5727373009088));
#155612=CARTESIAN_POINT('Ctrl Pts',(-19.8309999421957,-16.6389519834594,
15.5769070152291));
#155613=CARTESIAN_POINT('Ctrl Pts',(-19.7550173121369,-16.6029160083363,
15.5810765811732));
#155614=CARTESIAN_POINT('Ctrl Pts',(-19.6772558091333,-16.5706273036551,
15.5852461471172));
#155615=CARTESIAN_POINT('Ctrl Pts',(-19.5981218233864,-16.5422503295265,
15.5894157130613));
#155616=CARTESIAN_POINT('Ctrl Pts',(-19.516205584323,-16.5128756559943,
15.5937318758002));
#155617=CARTESIAN_POINT('Ctrl Pts',(-19.4328190502828,-16.4876930819298,
15.5980480385391));
#155618=CARTESIAN_POINT('Ctrl Pts',(-19.3484309915969,-16.4668290689441,
15.602364201278));
#155619=CARTESIAN_POINT('Ctrl Pts',(-19.2667918650466,-16.4466446989869,
15.6065397654697));
#155620=CARTESIAN_POINT('Ctrl Pts',(-19.1842159325101,-16.4305019005906,
15.6107153296614));
#155621=CARTESIAN_POINT('Ctrl Pts',(-19.1011369778115,-16.4184628600466,
15.6148908938531));
#155622=CARTESIAN_POINT('Ctrl Pts',(-19.0138619026127,-16.4058157561847,
15.6192773558656));
#155623=CARTESIAN_POINT('Ctrl Pts',(-18.9260322359069,-16.3976979204099,
15.6236638178782));
#155624=CARTESIAN_POINT('Ctrl Pts',(-18.8381534037013,-16.3941196141146,
15.6280502798907));
#155625=CARTESIAN_POINT('Ctrl Pts',(-18.7502745714957,-16.3905413078192,
15.6324367419032));
#155626=CARTESIAN_POINT('Ctrl Pts',(-18.6623471531411,-16.391502448601,
15.6368232039158));
#155627=CARTESIAN_POINT('Ctrl Pts',(-18.5748705298081,-16.3969505265619,
15.6412096659283));
#155628=CARTESIAN_POINT('Ctrl Pts',(-18.4914188355861,-16.4021479303798,
15.6453943003213));
#155629=CARTESIAN_POINT('Ctrl Pts',(-18.4080667413618,-16.4114477893304,
15.6495789347144));
#155630=CARTESIAN_POINT('Ctrl Pts',(-18.3252500890705,-16.4248428006325,
15.6537635691074));
#155631=CARTESIAN_POINT('Ctrl Pts',(-18.242551316033,-16.4382187457939,
15.6579422471914));
#155632=CARTESIAN_POINT('Ctrl Pts',(-18.1603869213347,-16.4556781923685,
15.6621209252753));
#155633=CARTESIAN_POINT('Ctrl Pts',(-18.079189748786,-16.4771619174368,
15.6662996033593));
#155634=CARTESIAN_POINT('Ctrl Pts',(-17.9965371752748,-16.4990307228369,
15.6705531812447));
#155635=CARTESIAN_POINT('Ctrl Pts',(-17.9148873210948,-16.5250694661818,
15.6748067591302));
#155636=CARTESIAN_POINT('Ctrl Pts',(-17.834688139716,-16.5551607943059,
15.6790603370156));
#155637=CARTESIAN_POINT('Ctrl Pts',(-17.756043775964,-16.5846687433158,
15.6832314509935));
#155638=CARTESIAN_POINT('Ctrl Pts',(-17.6787947892653,-16.618073375769,
15.6874025649715));
#155639=CARTESIAN_POINT('Ctrl Pts',(-17.6033486289325,-16.6552136631582,
15.6915736789494));
#155640=CARTESIAN_POINT('Ctrl Pts',(-17.5279277852875,-16.6923414877653,
15.6957433932698));
#155641=CARTESIAN_POINT('Ctrl Pts',(-17.4543089789465,-16.7332022747586,
15.6999131075902));
#155642=CARTESIAN_POINT('Ctrl Pts',(-17.3828779283351,-16.7775876316899,
15.7040828219106));
#155643=CARTESIAN_POINT('Ctrl Pts',(-17.311449419547,-16.8219714091997,
15.7082523878546));
#155644=CARTESIAN_POINT('Ctrl Pts',(-17.2422089019961,-16.8698792637608,
15.7124219537986));
#155645=CARTESIAN_POINT('Ctrl Pts',(-17.1755146319174,-16.9210585046653,
15.7165915197427));
#155646=CARTESIAN_POINT('Ctrl Pts',(-17.106475473579,-16.9740371445436,
15.7209076824816));
#155647=CARTESIAN_POINT('Ctrl Pts',(-17.0401653646942,-17.0305211737505,
15.7252238452205));
#155648=CARTESIAN_POINT('Ctrl Pts',(-16.9769443759542,-17.0901848818937,
15.7295400079594));
#155649=CARTESIAN_POINT('Ctrl Pts',(-16.9157828042729,-17.1479050510196,
15.7337155721511));
#155650=CARTESIAN_POINT('Ctrl Pts',(-16.8575124793693,-17.2086005517587,
15.7378911363428));
#155651=CARTESIAN_POINT('Ctrl Pts',(-16.8024204890299,-17.2719403008225,
15.7420667005345));
#155652=CARTESIAN_POINT('Ctrl Pts',(-16.7445459332272,-17.3384791900356,
15.746453162547));
#155653=CARTESIAN_POINT('Ctrl Pts',(-16.6901795852494,-17.4079360098511,
15.7508396245596));
#155654=CARTESIAN_POINT('Ctrl Pts',(-16.6396036508152,-17.4798913312797,
15.7552260865721));
#155655=CARTESIAN_POINT('Ctrl Pts',(-16.589027716381,-17.5518466527083,
15.7596125485847));
#155656=CARTESIAN_POINT('Ctrl Pts',(-16.5422424397947,-17.6262999440046,
15.7639990105972));
#155657=CARTESIAN_POINT('Ctrl Pts',(-16.4994739740979,-17.7028028820213,
15.7683854726097));
#155658=CARTESIAN_POINT('Ctrl Pts',(-16.458673348906,-17.7757858064552,
15.7725701070028));
#155659=CARTESIAN_POINT('Ctrl Pts',(-16.4213761508428,-17.8509055642073,
15.7767547413958));
#155660=CARTESIAN_POINT('Ctrl Pts',(-16.3878121523981,-17.9277917283262,
15.7809393757889));
#155661=CARTESIAN_POINT('Ctrl Pts',(-16.3542959281508,-18.004568454507,
15.7851180538728));
#155662=CARTESIAN_POINT('Ctrl Pts',(-16.3245025312236,-18.0831061749369,
15.7892967319568));
#155663=CARTESIAN_POINT('Ctrl Pts',(-16.2986164546585,-18.1630088802274,
15.7934754100407));
#155664=CARTESIAN_POINT('Ctrl Pts',(-16.272266388775,-18.2443437840853,
15.7977289879261));
#155665=CARTESIAN_POINT('Ctrl Pts',(-16.249965333752,-18.3270926679897,
15.8019825658115));
#155666=CARTESIAN_POINT('Ctrl Pts',(-16.2318570828658,-18.41081535292,15.806236143697));
#155667=CARTESIAN_POINT('Ctrl Pts',(-16.2140998957584,-18.4929149102316,
15.8104072576749));
#155668=CARTESIAN_POINT('Ctrl Pts',(-16.2003744938966,-18.575950377106,
15.8145783716529));
#155669=CARTESIAN_POINT('Ctrl Pts',(-16.1907660223746,-18.6594919914747,
15.8187494856308));
#155670=CARTESIAN_POINT('Ctrl Pts',(-16.1811607750679,-18.7430055726478,
15.8229191999512));
#155671=CARTESIAN_POINT('Ctrl Pts',(-16.1756697669882,-18.8270245073652,
15.8270889142716));
#155672=CARTESIAN_POINT('Ctrl Pts',(-16.1743265551335,-18.9111116685926,
15.8312586285919));
#155673=CARTESIAN_POINT('Ctrl Pts',(-16.172983391076,-18.9951958376379,
15.835428194536));
#155674=CARTESIAN_POINT('Ctrl Pts',(-16.1757877362795,-19.0793477683783,
15.83959776048));
#155675=CARTESIAN_POINT('Ctrl Pts',(-16.182721035153,-19.1631294473279,
15.8437673264241));
#155676=CARTESIAN_POINT('Ctrl Pts',(-16.1898981002616,-19.2498567867534,
15.848083489163));
#155677=CARTESIAN_POINT('Ctrl Pts',(-16.2014998257646,-19.3361868282285,
15.8523996519019));
#155678=CARTESIAN_POINT('Ctrl Pts',(-16.2174472402024,-19.4216405084265,
15.8567158146408));
#155679=CARTESIAN_POINT('Ctrl Pts',(-16.2328751692923,-19.5043105439801,
15.8608913788325));
#155680=CARTESIAN_POINT('Ctrl Pts',(-16.2523698584563,-19.5861599891139,
15.8650669430242));
#155681=CARTESIAN_POINT('Ctrl Pts',(-16.2758083142179,-19.6667682393277,
15.8692425072158));
#155682=CARTESIAN_POINT('Ctrl Pts',(-16.3004305906603,-19.7514478206318,
15.8736289692284));
#155683=CARTESIAN_POINT('Ctrl Pts',(-16.329405311324,-19.8347569748333,
15.8780154312409));
#155684=CARTESIAN_POINT('Ctrl Pts',(-16.3625325554081,-19.9162313826259,
15.8824018932535));
#155685=CARTESIAN_POINT('Ctrl Pts',(-16.3956597994922,-19.9977057904185,
15.886788355266));
#155686=CARTESIAN_POINT('Ctrl Pts',(-16.4329392521203,-20.0773449585574,
15.8911748172785));
#155687=CARTESIAN_POINT('Ctrl Pts',(-16.4741163568262,-20.1547160593073,
15.8955612792911));
#155688=CARTESIAN_POINT('Ctrl Pts',(-16.5134028649757,-20.2285347603028,
15.8997463422486));
#155689=CARTESIAN_POINT('Ctrl Pts',(-16.5563832077462,-20.3005638940195,
15.9039314052061));
#155690=CARTESIAN_POINT('Ctrl Pts',(-16.602870226229,-20.3704096331268,
15.9081164681637));
#155691=CARTESIAN_POINT('Ctrl Pts',(-16.6492791580943,-20.4401380487813,
15.9122945012573));
#155692=CARTESIAN_POINT('Ctrl Pts',(-16.6991828014366,-20.5076899821208,
15.916472534351));
#155693=CARTESIAN_POINT('Ctrl Pts',(-16.7523481443704,-20.5726961229916,
15.9206505674447));
#155694=CARTESIAN_POINT('Ctrl Pts',(-16.8054619536597,-20.637639252826,
15.9248245507334));
#155695=CARTESIAN_POINT('Ctrl Pts',(-16.861830896424,-20.700041135037,15.928998534022));
#155696=CARTESIAN_POINT('Ctrl Pts',(-16.9211791819455,-20.7595620823718,
15.9331725173107));
#155697=CARTESIAN_POINT('Ctrl Pts',(-16.9804837256674,-20.819039160649,
15.9373434242251));
#155698=CARTESIAN_POINT('Ctrl Pts',(-17.0427629244445,-20.8756391989201,
15.9415143311394));
#155699=CARTESIAN_POINT('Ctrl Pts',(-17.1077022600319,-20.9290573236441,
15.9456852380538));
#155700=CARTESIAN_POINT('Ctrl Pts',(-17.1296568439216,-20.9471168354927,
15.9470953314112));
#155701=CARTESIAN_POINT('Ctrl Pts',(-17.1519151618286,-20.9648129749097,
15.9485054247686));
#155702=CARTESIAN_POINT('Ctrl Pts',(-17.1744641402401,-20.9821349467765,
15.9499155181261));
#155703=CARTESIAN_POINT('Ctrl Pts',(-17.1744641402401,-20.9821349467764,
15.1499553790579));
#155704=CARTESIAN_POINT('Ctrl Pts',(-17.2409405369923,-21.0332016626749,
15.1541321105618));
#155705=CARTESIAN_POINT('Ctrl Pts',(-17.3100169746969,-21.0810682907154,
15.1583088420657));
#155706=CARTESIAN_POINT('Ctrl Pts',(-17.3813511233023,-21.125462908901,
15.1624855735696));
#155707=CARTESIAN_POINT('Ctrl Pts',(-17.4526153147779,-21.1698139894525,
15.1666582089688));
#155708=CARTESIAN_POINT('Ctrl Pts',(-17.5261324278215,-21.2106995852222,
15.1708308443679));
#155709=CARTESIAN_POINT('Ctrl Pts',(-17.6015297561884,-21.2478900554864,
15.1750034797671));
#155710=CARTESIAN_POINT('Ctrl Pts',(-17.6768875635137,-21.2850610316099,
15.1791739279946));
#155711=CARTESIAN_POINT('Ctrl Pts',(-17.7541232175784,-21.3185405247747,
15.1833443762221));
#155712=CARTESIAN_POINT('Ctrl Pts',(-17.8328389420969,-21.3481445590196,
15.1875148244496));
#155713=CARTESIAN_POINT('Ctrl Pts',(-17.9115370192045,-21.377741956286,
15.1916843376973));
#155714=CARTESIAN_POINT('Ctrl Pts',(-17.9917140771595,-21.4034654587896,
15.195853850945));
#155715=CARTESIAN_POINT('Ctrl Pts',(-18.0729531407356,-21.4251795425841,
15.2000233641926));
#155716=CARTESIAN_POINT('Ctrl Pts',(-18.1541983607488,-21.4468952719096,
15.2041931934133));
#155717=CARTESIAN_POINT('Ctrl Pts',(-18.2365053014123,-21.4646008616881,
15.2083630226339));
#155718=CARTESIAN_POINT('Ctrl Pts',(-18.3194439686069,-21.4782112534061,
15.2125328518545));
#155719=CARTESIAN_POINT('Ctrl Pts',(-18.4024694322536,-21.4918358885856,
15.2167070448586));
#155720=CARTESIAN_POINT('Ctrl Pts',(-18.4861274876637,-21.5013566932214,
15.2208812378627));
#155721=CARTESIAN_POINT('Ctrl Pts',(-18.5699806281551,-21.5067402305635,
15.2250554308667));
#155722=CARTESIAN_POINT('Ctrl Pts',(-18.6538791094179,-21.5121266788727,
15.2292318809256));
#155723=CARTESIAN_POINT('Ctrl Pts',(-18.7379724256015,-21.5133713983878,
15.2334083309844));
#155724=CARTESIAN_POINT('Ctrl Pts',(-18.821823103729,-21.5104931312105,
15.2375847810432));
#155725=CARTESIAN_POINT('Ctrl Pts',(-18.9058196496713,-21.5076098569593,
15.2417684965131));
#155726=CARTESIAN_POINT('Ctrl Pts',(-18.9895722555945,-21.5005893083999,
15.245952211983));
#155727=CARTESIAN_POINT('Ctrl Pts',(-19.072648815734,-21.4895021142064,
15.2501359274529));
#155728=CARTESIAN_POINT('Ctrl Pts',(-19.1358362944999,-21.4810692680884,
15.2533180335966));
#155729=CARTESIAN_POINT('Ctrl Pts',(-19.1986327885576,-21.4702849361346,
15.2565001397403));
#155730=CARTESIAN_POINT('Ctrl Pts',(-19.2608535512399,-21.4571996598167,
15.259682245884));
#155731=CARTESIAN_POINT('Ctrl Pts',(-19.3426770768309,-21.4399918437197,
15.263866880277));
#155732=CARTESIAN_POINT('Ctrl Pts',(-19.4238089369639,-21.4187390730901,
15.2680515146701));
#155733=CARTESIAN_POINT('Ctrl Pts',(-19.5038189245161,-21.3935115857716,
15.2722361490631));
#155734=CARTESIAN_POINT('Ctrl Pts',(-19.5837150277544,-21.3683200066587,
15.2764148271471));
#155735=CARTESIAN_POINT('Ctrl Pts',(-19.6624919952641,-21.33916508562,15.280593505231));
#155736=CARTESIAN_POINT('Ctrl Pts',(-19.7397300928954,-21.3061680017035,
15.284772183315));
#155737=CARTESIAN_POINT('Ctrl Pts',(-19.8183526279167,-21.2725794687723,
15.2890257612004));
#155738=CARTESIAN_POINT('Ctrl Pts',(-19.8953801101215,-21.2350097758302,
15.2932793390858));
#155739=CARTESIAN_POINT('Ctrl Pts',(-19.9703862586167,-21.1936398059242,
15.2975329169713));
#155740=CARTESIAN_POINT('Ctrl Pts',(-20.0439382665608,-21.1530718736117,
15.3017040309492));
#155741=CARTESIAN_POINT('Ctrl Pts',(-20.1155461950122,-21.1088499333759,
15.3058751449272));
#155742=CARTESIAN_POINT('Ctrl Pts',(-20.1848301560489,-21.0611922288637,
15.3100462589051));
#155743=CARTESIAN_POINT('Ctrl Pts',(-20.2540908681833,-21.0135505163546,
15.3142159732255));
#155744=CARTESIAN_POINT('Ctrl Pts',(-20.3210287829501,-20.9624755897522,
15.3183856875459));
#155745=CARTESIAN_POINT('Ctrl Pts',(-20.385292362642,-20.9082294172924,
15.3225554018662));
#155746=CARTESIAN_POINT('Ctrl Pts',(-20.4495536555601,-20.8539851751442,
15.3267249678103));
#155747=CARTESIAN_POINT('Ctrl Pts',(-20.511140451629,-20.7965702088955,
15.3308945337543));
#155748=CARTESIAN_POINT('Ctrl Pts',(-20.5697347912253,-20.7362863492963,
15.3350640996984));
#155749=CARTESIAN_POINT('Ctrl Pts',(-20.6303892355178,-20.6738829835618,
15.3393802624373));
#155750=CARTESIAN_POINT('Ctrl Pts',(-20.6878365109499,-20.6084056085288,
15.3436964251762));
#155751=CARTESIAN_POINT('Ctrl Pts',(-20.7417674193153,-20.5402285698022,
15.3480125879151));
#155752=CARTESIAN_POINT('Ctrl Pts',(-20.7939415340131,-20.4742723909413,
15.3521881521068));
#155753=CARTESIAN_POINT('Ctrl Pts',(-20.8428246196126,-20.4057901412951,
15.3563637162985));
#155754=CARTESIAN_POINT('Ctrl Pts',(-20.8881804708297,-20.3351509314228,
15.3605392804902));
#155755=CARTESIAN_POINT('Ctrl Pts',(-20.9358271382687,-20.2609439029885,
15.3649257425027));
#155756=CARTESIAN_POINT('Ctrl Pts',(-20.9795805961807,-20.1843567987732,
15.3693122045153));
#155757=CARTESIAN_POINT('Ctrl Pts',(-21.0192222426252,-20.1058454410409,
15.3736986665278));
#155758=CARTESIAN_POINT('Ctrl Pts',(-21.0588638890698,-20.0273340833086,
15.3780851285404));
#155759=CARTESIAN_POINT('Ctrl Pts',(-21.0943935591862,-19.9468990335383,
15.3824715905529));
#155760=CARTESIAN_POINT('Ctrl Pts',(-21.1256522921828,-19.8650166007783,
15.3868580525655));
#155761=CARTESIAN_POINT('Ctrl Pts',(-21.1596866697226,-19.7758633510054,
15.3916340140293));
#155762=CARTESIAN_POINT('Ctrl Pts',(-21.1887650239783,-19.6847190703918,
15.3964099754931));
#155763=CARTESIAN_POINT('Ctrl Pts',(-21.2126811308614,-19.5921092496689,
15.4011859369569));
#155764=CARTESIAN_POINT('Ctrl Pts',(-21.2364993763692,-19.4998783754223,
15.4059423558521));
#155765=CARTESIAN_POINT('Ctrl Pts',(-21.2551974088384,-19.4061941121839,
15.4106987747474));
#155766=CARTESIAN_POINT('Ctrl Pts',(-21.2686182636666,-19.3115973546727,
15.4154551936427));
#155767=CARTESIAN_POINT('Ctrl Pts',(-21.2819450244391,-19.2176638181475,
15.4201782651282));
#155768=CARTESIAN_POINT('Ctrl Pts',(-21.2900682365862,-19.1228307363249,
15.4249013366138));
#155769=CARTESIAN_POINT('Ctrl Pts',(-21.2928821031965,-19.0276464271503,
15.4296244080994));
#155770=CARTESIAN_POINT('Ctrl Pts',(-21.2936100754836,-19.0030214008636,
15.4308463086468));
#155771=CARTESIAN_POINT('Ctrl Pts',(-21.2939829474075,-18.9783729560409,
15.4320682091942));
#155772=CARTESIAN_POINT('Ctrl Pts',(-21.293999428374,-18.9537107672549,
15.4332901097416));
#155773=CARTESIAN_POINT('',(-21.2939991231355,-18.9498811452879,15.3667098902285));
#155774=CARTESIAN_POINT('Ctrl Pts',(-17.1744641402401,-20.9821349467765,
15.0832685784559));
#155775=CARTESIAN_POINT('Ctrl Pts',(-17.2419504786654,-21.0339774929999,
15.0874896131755));
#155776=CARTESIAN_POINT('Ctrl Pts',(-17.3119988557323,-21.0824315373856,
15.0917106478951));
#155777=CARTESIAN_POINT('Ctrl Pts',(-17.3842279220291,-21.1272506378645,
15.0959316826146));
#155778=CARTESIAN_POINT('Ctrl Pts',(-17.4556818103574,-21.1715887300592,
15.1001074162762));
#155779=CARTESIAN_POINT('Ctrl Pts',(-17.5292693675069,-21.2123693557197,
15.1042831499379));
#155780=CARTESIAN_POINT('Ctrl Pts',(-17.6045968204046,-21.2494003695307,
15.1084588835995));
#155781=CARTESIAN_POINT('Ctrl Pts',(-17.6811500746533,-21.2870339879037,
15.112702568848));
#155782=CARTESIAN_POINT('Ctrl Pts',(-17.7594999004546,-21.3207946763895,
15.1169462540966));
#155783=CARTESIAN_POINT('Ctrl Pts',(-17.8392139384063,-21.3505324479727,
15.1211899393451));
#155784=CARTESIAN_POINT('Ctrl Pts',(-17.9189279763581,-21.3802702195558,
15.1254336245937));
#155785=CARTESIAN_POINT('Ctrl Pts',(-18.000005738032,-21.4059849886204,
15.1296773098422));
#155786=CARTESIAN_POINT('Ctrl Pts',(-18.0820028534413,-21.4275806835729,
15.1339209950908));
#155787=CARTESIAN_POINT('Ctrl Pts',(-18.1628589794675,-21.4488758745561,
15.1381056294838));
#155788=CARTESIAN_POINT('Ctrl Pts',(-18.2449099711163,-21.4662452083818,
15.1422902638769));
#155789=CARTESIAN_POINT('Ctrl Pts',(-18.3277397785898,-21.4795586308728,
15.1464748982699));
#155790=CARTESIAN_POINT('Ctrl Pts',(-18.4104516880846,-21.4928531033548,
15.1506535763538));
#155791=CARTESIAN_POINT('Ctrl Pts',(-18.4939397611609,-21.5021030592902,
15.1548322544378));
#155792=CARTESIAN_POINT('Ctrl Pts',(-18.5777744755002,-21.5072286757734,
15.1590109325217));
#155793=CARTESIAN_POINT('Ctrl Pts',(-18.6631118668432,-21.5124461652484,
15.1632645104072));
#155794=CARTESIAN_POINT('Ctrl Pts',(-18.7488079825307,-21.5133898805874,
15.1675180882926));
#155795=CARTESIAN_POINT('Ctrl Pts',(-18.8344006857365,-21.510030434202,
15.171771666178));
#155796=CARTESIAN_POINT('Ctrl Pts',(-18.9183340073703,-21.5067361172402,
15.175942780156));
#155797=CARTESIAN_POINT('Ctrl Pts',(-19.0021674095972,-21.4993040188572,
15.1801138941339));
#155798=CARTESIAN_POINT('Ctrl Pts',(-19.0854634797585,-21.4877589440631,
15.1842850081119));
#155799=CARTESIAN_POINT('Ctrl Pts',(-19.1687315991189,-21.4762177433303,
15.1884547224322));
#155800=CARTESIAN_POINT('Ctrl Pts',(-19.2514622892087,-21.4605663702897,
15.1926244367526));
#155801=CARTESIAN_POINT('Ctrl Pts',(-19.3332238803096,-21.4408814237056,
15.196794151073));
#155802=CARTESIAN_POINT('Ctrl Pts',(-19.4149825619822,-21.4211971775964,
15.200963717017));
#155803=CARTESIAN_POINT('Ctrl Pts',(-19.4957717661771,-21.3974797518312,
15.2051332829611));
#155804=CARTESIAN_POINT('Ctrl Pts',(-19.5751719705272,-21.3698564299808,
15.2093028489051));
#155805=CARTESIAN_POINT('Ctrl Pts',(-19.6573637881115,-21.3412619062112,
15.2136190116441));
#155806=CARTESIAN_POINT('Ctrl Pts',(-19.7380666159169,-21.3084818866878,
15.217935174383));
#155807=CARTESIAN_POINT('Ctrl Pts',(-19.8168362586924,-21.2717124039115,
15.2222513371219));
#155808=CARTESIAN_POINT('Ctrl Pts',(-19.8930399886396,-21.2361406831692,
15.2264269013136));
#155809=CARTESIAN_POINT('Ctrl Pts',(-19.9674341519886,-21.1968356830555,
15.2306024655052));
#155810=CARTESIAN_POINT('Ctrl Pts',(-20.0396421490703,-21.1540214755018,
15.2347780296969));
#155811=CARTESIAN_POINT('Ctrl Pts',(-20.1154972004264,-21.1090448241057,
15.2391644917094));
#155812=CARTESIAN_POINT('Ctrl Pts',(-20.188938948885,-21.0601954720668,
15.243550953722));
#155813=CARTESIAN_POINT('Ctrl Pts',(-20.259567662025,-21.0077828943212,
15.2479374157345));
#155814=CARTESIAN_POINT('Ctrl Pts',(-20.330196375165,-20.9553703165755,
15.252323877747));
#155815=CARTESIAN_POINT('Ctrl Pts',(-20.398011653933,-20.899394941135,15.2567103397596));
#155816=CARTESIAN_POINT('Ctrl Pts',(-20.4626578964185,-20.8402112903883,
15.2610968017721));
#155817=CARTESIAN_POINT('Ctrl Pts',(-20.5234100187943,-20.7845927075509,
15.2652190348167));
#155818=CARTESIAN_POINT('Ctrl Pts',(-20.5816044022752,-20.7259204795934,
15.2693412678613));
#155819=CARTESIAN_POINT('Ctrl Pts',(-20.6369112461382,-20.6644627847987,
15.2734635009059));
#155820=CARTESIAN_POINT('Ctrl Pts',(-20.6921256485478,-20.6031078121671,
15.2775788439313));
#155821=CARTESIAN_POINT('Ctrl Pts',(-20.7444617859852,-20.538976972769,
15.2816941869567));
#155822=CARTESIAN_POINT('Ctrl Pts',(-20.7936245240703,-20.4723771965695,
15.2858095299821));
#155823=CARTESIAN_POINT('Ctrl Pts',(-20.8427410076358,-20.4058400804406,
15.2899210011074));
#155824=CARTESIAN_POINT('Ctrl Pts',(-20.888689733586,-20.3368390147958,
15.2940324722326));
#155825=CARTESIAN_POINT('Ctrl Pts',(-20.9312146121388,-20.26571532236,15.2981439433578));
#155826=CARTESIAN_POINT('Ctrl Pts',(-20.9737131282065,-20.1946357216972,
15.3022528656552));
#155827=CARTESIAN_POINT('Ctrl Pts',(-21.0127917657816,-20.1214365120737,
15.3063617879525));
#155828=CARTESIAN_POINT('Ctrl Pts',(-21.0482376124058,-20.0464881330222,
15.3104707102499));
#155829=CARTESIAN_POINT('Ctrl Pts',(-21.0836728562216,-19.9715621730513,
15.3145784034578));
#155830=CARTESIAN_POINT('Ctrl Pts',(-21.1154772648505,-19.8948885121031,
15.3186860966657));
#155831=CARTESIAN_POINT('Ctrl Pts',(-21.1434845038947,-19.8168609284106,
15.3227937898736));
#155832=CARTESIAN_POINT('Ctrl Pts',(-21.1715053065238,-19.7387955568538,
15.3269034723903));
#155833=CARTESIAN_POINT('Ctrl Pts',(-21.1957251016683,-19.6593753990475,
15.3310131549069));
#155834=CARTESIAN_POINT('Ctrl Pts',(-21.2160265895469,-19.5790119686115,
15.3351228374236));
#155835=CARTESIAN_POINT('Ctrl Pts',(-21.2363332616042,-19.4986280166064,
15.3392335693869));
#155836=CARTESIAN_POINT('Ctrl Pts',(-21.2527195357624,-19.4173007774455,
15.3433443013502));
#155837=CARTESIAN_POINT('Ctrl Pts',(-21.265119175788,-19.3354523672614,
15.3474550333135));
#155838=CARTESIAN_POINT('Ctrl Pts',(-21.277533866187,-19.2535046115213,
15.3515707547806));
#155839=CARTESIAN_POINT('Ctrl Pts',(-21.2859522113271,-19.1710348943524,
15.3556864762477));
#155840=CARTESIAN_POINT('Ctrl Pts',(-21.2903598951029,-19.0884700945603,
15.3598021977147));
#155841=CARTESIAN_POINT('Ctrl Pts',(-21.2928257992759,-19.0422787399392,
15.362104761886));
#155842=CARTESIAN_POINT('Ctrl Pts',(-21.294037342402,-18.9960576424384,
15.3644073260573));
#155843=CARTESIAN_POINT('Ctrl Pts',(-21.2939991231355,-18.9498811452879,
15.3667098902285));
#155844=CARTESIAN_POINT('Ctrl Pts',(-21.2956373739999,-18.9498797893439,
15.3667098902285));
#155845=CARTESIAN_POINT('Ctrl Pts',(-21.296922788715,-18.8056440679786,
15.3738974629702));
#155846=CARTESIAN_POINT('Ctrl Pts',(-21.2201491749354,-17.8120820090192,
15.4234769712724));
#155847=CARTESIAN_POINT('Ctrl Pts',(-19.9200692397814,-16.166945137558,
15.515448415135));
#155848=CARTESIAN_POINT('Ctrl Pts',(-17.0342063890851,-16.4472060945738,
15.6426242218164));
#155849=CARTESIAN_POINT('Ctrl Pts',(-15.7555915863648,-18.9325607617256,
15.7652176501285));
#155850=CARTESIAN_POINT('Ctrl Pts',(-16.5753465902488,-20.5182929546658,
15.84541914288));
#155851=CARTESIAN_POINT('Ctrl Pts',(-17.172599330006,-20.9845253206546,
15.883228700071));
#155852=CARTESIAN_POINT('Origin',(-18.734,-18.952,-1.76670989022851));
#155853=CARTESIAN_POINT('',(-17.1744641402402,-20.9821349467765,16.7498176584939));
#155854=CARTESIAN_POINT('',(-17.1744641402401,-20.9821349467765,16.6833822503202));
#155855=CARTESIAN_POINT('',(-17.1744641402401,-20.9821349467765,-1.76670989022851));
#155856=CARTESIAN_POINT('',(-21.2939992944986,-18.9500994299065,16.2332901098004));
#155857=CARTESIAN_POINT('Ctrl Pts',(-21.2939992944986,-18.9500994299065,
16.2332901098004));
#155858=CARTESIAN_POINT('Ctrl Pts',(-21.2939272486892,-18.8530563258845,
16.2381006886061));
#155859=CARTESIAN_POINT('Ctrl Pts',(-21.2883332378637,-18.7562381388316,
16.2429112674119));
#155860=CARTESIAN_POINT('Ctrl Pts',(-21.277317503626,-18.6602191305971,
16.2477218462176));
#155861=CARTESIAN_POINT('Ctrl Pts',(-21.2661096544806,-18.5625255464771,
16.2526163217373));
#155862=CARTESIAN_POINT('Ctrl Pts',(-21.2492893600035,-18.4656594493969,
16.2575107972569));
#155863=CARTESIAN_POINT('Ctrl Pts',(-21.2270132516535,-18.3702054253606,
16.2624052727766));
#155864=CARTESIAN_POINT('Ctrl Pts',(-21.2047371433035,-18.2747514013242,
16.2672997482962));
#155865=CARTESIAN_POINT('Ctrl Pts',(-21.1770053785921,-18.1807095711097,
16.2721942238158));
#155866=CARTESIAN_POINT('Ctrl Pts',(-21.1440235064311,-18.088642195582,
16.2770886993355));
#155867=CARTESIAN_POINT('Ctrl Pts',(-21.1158249638011,-18.0099272639074,
16.2812733337285));
#155868=CARTESIAN_POINT('Ctrl Pts',(-21.0837134704203,-17.9324488089605,
16.2854579681216));
#155869=CARTESIAN_POINT('Ctrl Pts',(-21.0478172393664,-17.856623451588,
16.2896426025146));
#155870=CARTESIAN_POINT('Ctrl Pts',(-21.0119721021543,-17.7809060222264,
16.2938212805986));
#155871=CARTESIAN_POINT('Ctrl Pts',(-20.9723531229121,-17.7068374289185,
16.2979999586825));
#155872=CARTESIAN_POINT('Ctrl Pts',(-20.9291375533229,-17.6348169747558,
16.3021786367665));
#155873=CARTESIAN_POINT('Ctrl Pts',(-20.8851473757074,-17.5615056057125,
16.3064322146519));
#155874=CARTESIAN_POINT('Ctrl Pts',(-20.8374305643562,-17.4903169777088,
16.3106857925373));
#155875=CARTESIAN_POINT('Ctrl Pts',(-20.7862244101174,-17.4216487427658,
16.3149393704228));
#155876=CARTESIAN_POINT('Ctrl Pts',(-20.7360109870992,-17.3543117755523,
16.3191104844007));
#155877=CARTESIAN_POINT('Ctrl Pts',(-20.6824425969515,-17.2893987337786,
16.3232815983787));
#155878=CARTESIAN_POINT('Ctrl Pts',(-20.6257872198942,-17.2272562176819,
16.3274527123566));
#155879=CARTESIAN_POINT('Ctrl Pts',(-20.5691508540959,-17.1651345541068,
16.331622426677));
#155880=CARTESIAN_POINT('Ctrl Pts',(-20.5094298683179,-17.105781909528,
16.3357921409974));
#155881=CARTESIAN_POINT('Ctrl Pts',(-20.4469316957118,-17.0495108394984,
16.3399618553177));
#155882=CARTESIAN_POINT('Ctrl Pts',(-20.3844357470588,-16.993241771835,
16.3441314212618));
#155883=CARTESIAN_POINT('Ctrl Pts',(-20.3191631505139,-16.9400543678782,
16.3483009872058));
#155884=CARTESIAN_POINT('Ctrl Pts',(-20.2514562536418,-16.890222485746,
16.3524705531499));
#155885=CARTESIAN_POINT('Ctrl Pts',(-20.1813688658012,-16.8386385761122,
16.3567867158888));
#155886=CARTESIAN_POINT('Ctrl Pts',(-20.108673237446,-16.7906508514966,
16.3611028786277));
#155887=CARTESIAN_POINT('Ctrl Pts',(-20.0337823603675,-16.7465146076935,
16.3654190413666));
#155888=CARTESIAN_POINT('Ctrl Pts',(-19.9613310457328,-16.7038160973899,
16.3695946055583));
#155889=CARTESIAN_POINT('Ctrl Pts',(-19.8868257455389,-16.6647221743667,
16.37377016975));
#155890=CARTESIAN_POINT('Ctrl Pts',(-19.8106643175706,-16.6294165359948,
16.3779457339417));
#155891=CARTESIAN_POINT('Ctrl Pts',(-19.7306561569322,-16.59232769376,16.3823321959542));
#155892=CARTESIAN_POINT('Ctrl Pts',(-19.6488207114385,-16.5594201038734,
16.3867186579667));
#155893=CARTESIAN_POINT('Ctrl Pts',(-19.5656393424726,-16.5308482071436,
16.3911051199793));
#155894=CARTESIAN_POINT('Ctrl Pts',(-19.4824579735068,-16.5022763104138,
16.3954915819918));
#155895=CARTESIAN_POINT('Ctrl Pts',(-19.3979312597771,-16.4780401936422,
16.3998780440044));
#155896=CARTESIAN_POINT('Ctrl Pts',(-19.3125527301389,-16.4582324209244,
16.4042645060169));
#155897=CARTESIAN_POINT('Ctrl Pts',(-19.2311025932107,-16.4393360331914,
16.4084491404099));
#155898=CARTESIAN_POINT('Ctrl Pts',(-19.1485741315074,-16.4243990992031,
16.412633774803));
#155899=CARTESIAN_POINT('Ctrl Pts',(-19.0653870565365,-16.4135393210136,
16.416818409196));
#155900=CARTESIAN_POINT('Ctrl Pts',(-18.9823183880704,-16.4026950003742,
16.42099708728));
#155901=CARTESIAN_POINT('Ctrl Pts',(-18.8985934206771,-16.3959163673419,
16.4251757653639));
#155902=CARTESIAN_POINT('Ctrl Pts',(-18.8146438480398,-16.393270516492,
16.4293544434479));
#155903=CARTESIAN_POINT('Ctrl Pts',(-18.7291895396465,-16.390577240667,
16.4336080213333));
#155904=CARTESIAN_POINT('Ctrl Pts',(-18.6435029643765,-16.392166473525,
16.4378615992187));
#155905=CARTESIAN_POINT('Ctrl Pts',(-18.5580469256853,-16.3980539325117,
16.4421151771042));
#155906=CARTESIAN_POINT('Ctrl Pts',(-18.4742476190579,-16.4038272516174,
16.4462862910821));
#155907=CARTESIAN_POINT('Ctrl Pts',(-18.3906704700557,-16.4137335920112,
16.4504574050601));
#155908=CARTESIAN_POINT('Ctrl Pts',(-18.307751967238,-16.4277352328715,
16.454628519038));
#155909=CARTESIAN_POINT('Ctrl Pts',(-18.2248612885247,-16.4417321753459,
16.4587982333584));
#155910=CARTESIAN_POINT('Ctrl Pts',(-18.1426292702901,-16.4598216125358,
16.4629679476788));
#155911=CARTESIAN_POINT('Ctrl Pts',(-18.0614851300251,-16.4819142222055,
16.4671376619991));
#155912=CARTESIAN_POINT('Ctrl Pts',(-17.9803438772167,-16.5040060457254,
16.4713072279432));
#155913=CARTESIAN_POINT('Ctrl Pts',(-17.9002908690612,-16.5301006368245,
16.4754767938872));
#155914=CARTESIAN_POINT('Ctrl Pts',(-17.8217416831402,-16.5600583695834,
16.4796463598313));
#155915=CARTESIAN_POINT('Ctrl Pts',(-17.7404308047433,-16.5910693792692,
16.4839625225702));
#155916=CARTESIAN_POINT('Ctrl Pts',(-17.6607319577165,-16.6262200532081,
16.4882786853091));
#155917=CARTESIAN_POINT('Ctrl Pts',(-17.5830833500453,-16.6653013174323,
16.492594848048));
#155918=CARTESIAN_POINT('Ctrl Pts',(-17.5079641376018,-16.703109513585,
16.4967704122397));
#155919=CARTESIAN_POINT('Ctrl Pts',(-17.4347640291965,-16.7445958812711,
16.5009459764314));
#155920=CARTESIAN_POINT('Ctrl Pts',(-17.3638528381206,-16.7895253169588,
16.5051215406231));
#155921=CARTESIAN_POINT('Ctrl Pts',(-17.2893600913589,-16.8367240316336,
16.5095080026356));
#155922=CARTESIAN_POINT('Ctrl Pts',(-17.2173940414895,-16.8877224362901,
16.5138944646482));
#155923=CARTESIAN_POINT('Ctrl Pts',(-17.1483451005787,-16.9421993780623,
16.5182809266607));
#155924=CARTESIAN_POINT('Ctrl Pts',(-17.0792961596678,-16.9966763198346,
16.5226673886732));
#155925=CARTESIAN_POINT('Ctrl Pts',(-17.0131647139456,-17.0546313591046,
16.5270538506858));
#155926=CARTESIAN_POINT('Ctrl Pts',(-16.9502957329766,-17.115699619397,
16.5314403126983));
#155927=CARTESIAN_POINT('Ctrl Pts',(-16.8903194470162,-17.1739580385086,
16.5356249470914));
#155928=CARTESIAN_POINT('Ctrl Pts',(-16.8330887583091,-17.2352663353223,
16.5398095814844));
#155929=CARTESIAN_POINT('Ctrl Pts',(-16.7789298175348,-17.2993353087708,
16.5439942158775));
#155930=CARTESIAN_POINT('Ctrl Pts',(-16.7248479653093,-17.3633130879657,
16.5481728939614));
#155931=CARTESIAN_POINT('Ctrl Pts',(-16.6738294707906,-17.4300433902867,
16.5523515720454));
#155932=CARTESIAN_POINT('Ctrl Pts',(-16.6261644175018,-17.4991995466842,
16.5565302501293));
#155933=CARTESIAN_POINT('Ctrl Pts',(-16.577645002389,-17.5695952774835,
16.5607838280147));
#155934=CARTESIAN_POINT('Ctrl Pts',(-16.5326007777018,-17.6425043486949,
16.5650374059002));
#155935=CARTESIAN_POINT('Ctrl Pts',(-16.4912954660574,-17.7175461234078,
16.5692909837856));
#155936=CARTESIAN_POINT('Ctrl Pts',(-16.45079093848,-17.791133066886,16.5734620977636));
#155937=CARTESIAN_POINT('Ctrl Pts',(-16.4138818774499,-17.8667703369927,
16.5776332117415));
#155938=CARTESIAN_POINT('Ctrl Pts',(-16.3807728287042,-17.9440704983605,
16.5818043257195));
#155939=CARTESIAN_POINT('Ctrl Pts',(-16.3476748900196,-18.0213447209125,
16.5859740400399));
#155940=CARTESIAN_POINT('Ctrl Pts',(-16.318374612164,-18.1002803040064,
16.5901437543602));
#155941=CARTESIAN_POINT('Ctrl Pts',(-16.2930292165598,-18.1804679952255,
16.5943134686806));
#155942=CARTESIAN_POINT('Ctrl Pts',(-16.2676847228536,-18.2606528330224,
16.5984830346246));
#155943=CARTESIAN_POINT('Ctrl Pts',(-16.2462949694201,-18.3420892514569,
16.6026526005687));
#155944=CARTESIAN_POINT('Ctrl Pts',(-16.2289674972205,-18.4243522386873,
16.6068221665127));
#155945=CARTESIAN_POINT('Ctrl Pts',(-16.2110308124741,-18.5095074910663,
16.6111383292517));
#155946=CARTESIAN_POINT('Ctrl Pts',(-16.1974474922546,-18.5955480019176,
16.6154544919906));
#155947=CARTESIAN_POINT('Ctrl Pts',(-16.1882789321129,-18.6819921399002,
16.6197706547295));
#155948=CARTESIAN_POINT('Ctrl Pts',(-16.1794090368535,-18.7656203691804,
16.6239462189212));
#155949=CARTESIAN_POINT('Ctrl Pts',(-16.1746706763875,-18.8496258601583,
16.6281217831129));
#155950=CARTESIAN_POINT('Ctrl Pts',(-16.1740663387713,-18.9335704012975,
16.6322973473045));
#155951=CARTESIAN_POINT('Ctrl Pts',(-16.1734314774988,-19.0217547816503,
16.6366838093171));
#155952=CARTESIAN_POINT('Ctrl Pts',(-16.1773592072922,-19.1098713098955,
16.6410702713296));
#155953=CARTESIAN_POINT('Ctrl Pts',(-16.1857908120614,-19.1974178773141,
16.6454567333422));
#155954=CARTESIAN_POINT('Ctrl Pts',(-16.1942224168306,-19.2849644447327,
16.6498431953547));
#155955=CARTESIAN_POINT('Ctrl Pts',(-16.2071577359856,-19.3719404886095,
16.6542296573672));
#155956=CARTESIAN_POINT('Ctrl Pts',(-16.2244766916358,-19.4578584434176,
16.6586161193798));
#155957=CARTESIAN_POINT('Ctrl Pts',(-16.2409948213726,-19.539803564873,
16.6627997520463));
#155958=CARTESIAN_POINT('Ctrl Pts',(-16.2615616142029,-19.6210912295922,
16.6669833847129));
#155959=CARTESIAN_POINT('Ctrl Pts',(-16.2861104910148,-19.7012909660474,
16.6711670173794));
#155960=CARTESIAN_POINT('Ctrl Pts',(-16.3106270618244,-19.7813851606933,
16.6753451444398));
#155961=CARTESIAN_POINT('Ctrl Pts',(-16.339115179781,-19.8603938336953,
16.6795232715002));
#155962=CARTESIAN_POINT('Ctrl Pts',(-16.3714572466738,-19.9378964137807,
16.6837013985606));
#155963=CARTESIAN_POINT('Ctrl Pts',(-16.4037664575643,-20.0153202597224,
16.6878752811009));
#155964=CARTESIAN_POINT('Ctrl Pts',(-16.4399216659544,-20.0912406291382,
16.6920491636412));
#155965=CARTESIAN_POINT('Ctrl Pts',(-16.4797558270926,-20.1652531512068,
16.6962230461816));
#155966=CARTESIAN_POINT('Ctrl Pts',(-16.5195614728711,-20.2392126912711,
16.7003939408402));
#155967=CARTESIAN_POINT('Ctrl Pts',(-16.563040621407,-20.3112666936583,
16.7045648354988));
#155968=CARTESIAN_POINT('Ctrl Pts',(-16.6099791482511,-20.3810330371743,
16.7087357301574));
#155969=CARTESIAN_POINT('Ctrl Pts',(-16.656906125228,-20.4507822137264,
16.7129055985102));
#155970=CARTESIAN_POINT('Ctrl Pts',(-16.707290538528,-20.5182444646104,
16.7170754668631));
#155971=CARTESIAN_POINT('Ctrl Pts',(-16.7608741705717,-20.5830654374497,
16.721245335216));
#155972=CARTESIAN_POINT('Ctrl Pts',(-16.814450725416,-20.6478778488882,
16.7254146528225));
#155973=CARTESIAN_POINT('Ctrl Pts',(-16.8712253612539,-20.7100493251438,
16.729583970429));
#155974=CARTESIAN_POINT('Ctrl Pts',(-16.9308997149153,-20.7692587493055,
16.7337532880356));
#155975=CARTESIAN_POINT('Ctrl Pts',(-16.9906010255816,-20.8284949204471,
16.7379244890695));
#155976=CARTESIAN_POINT('Ctrl Pts',(-17.0532043371944,-20.8847660495707,
16.7420956901035));
#155977=CARTESIAN_POINT('Ctrl Pts',(-17.1183753222518,-20.9377887351506,
16.7462668911375));
#155978=CARTESIAN_POINT('Ctrl Pts',(-17.1368677583985,-20.9528340597924,
16.7474504802563));
#155979=CARTESIAN_POINT('Ctrl Pts',(-17.1555667305739,-20.9676180851866,
16.7486340693751));
#155980=CARTESIAN_POINT('Ctrl Pts',(-17.1744641402402,-20.9821349467765,
16.7498176584939));
#155981=CARTESIAN_POINT('Ctrl Pts',(-17.1744641402401,-20.9821349467765,
15.9499155181261));
#155982=CARTESIAN_POINT('Ctrl Pts',(-17.2411396316843,-21.0333546058634,
15.9540850492628));
#155983=CARTESIAN_POINT('Ctrl Pts',(-17.3103587055251,-21.0812996420495,
15.9582545803995));
#155984=CARTESIAN_POINT('Ctrl Pts',(-17.3817621512649,-21.1257186571514,
15.9624241115362));
#155985=CARTESIAN_POINT('Ctrl Pts',(-17.4531698880323,-21.1701403416375,
15.9665938932431));
#155986=CARTESIAN_POINT('Ctrl Pts',(-17.5267618660371,-21.2110353423976,
15.97076367495));
#155987=CARTESIAN_POINT('Ctrl Pts',(-17.6021516704121,-21.2481967160522,
15.9749334566569));
#155988=CARTESIAN_POINT('Ctrl Pts',(-17.6776196576944,-21.2853966278654,
15.979107562631));
#155989=CARTESIAN_POINT('Ctrl Pts',(-17.7548887811624,-21.3188549763378,
15.983281668605));
#155990=CARTESIAN_POINT('Ctrl Pts',(-17.8335503409496,-21.3484119870164,
15.9874557745791));
#155991=CARTESIAN_POINT('Ctrl Pts',(-17.9122533278425,-21.377984563893,
15.9916320788458));
#155992=CARTESIAN_POINT('Ctrl Pts',(-17.9923497730624,-21.4036515707366,
15.9958083831126));
#155993=CARTESIAN_POINT('Ctrl Pts',(-18.0734157506516,-21.4253031454945,
15.9999846873793));
#155994=CARTESIAN_POINT('Ctrl Pts',(-18.1546240863822,-21.4469927420961,
16.0041683255601));
#155995=CARTESIAN_POINT('Ctrl Pts',(-18.2368049051917,-21.4646527238166,
16.0083519637409));
#155996=CARTESIAN_POINT('Ctrl Pts',(-18.3195242010686,-21.478224418396,
16.0125356019217));
#155997=CARTESIAN_POINT('Ctrl Pts',(-18.3867591085121,-21.4892556006519,
16.0159360966053));
#155998=CARTESIAN_POINT('Ctrl Pts',(-18.4543495129699,-21.4975868065142,
16.019336591289));
#155999=CARTESIAN_POINT('Ctrl Pts',(-18.5220617179685,-21.5032119011579,
16.0227370859726));
#156000=CARTESIAN_POINT('Ctrl Pts',(-18.605388071405,-21.5101341188644,
16.0269217203656));
#156001=CARTESIAN_POINT('Ctrl Pts',(-18.6892089831259,-21.5129825827272,
16.0311063547587));
#156002=CARTESIAN_POINT('Ctrl Pts',(-18.7730921344112,-21.5117015070174,
16.0352909891517));
#156003=CARTESIAN_POINT('Ctrl Pts',(-18.8568558884132,-21.5104222547604,
16.0394696672357));
#156004=CARTESIAN_POINT('Ctrl Pts',(-18.9406812499664,-21.5050251452316,
16.0436483453196));
#156005=CARTESIAN_POINT('Ctrl Pts',(-19.0241313606306,-21.4955062008139,
16.0478270234036));
#156006=CARTESIAN_POINT('Ctrl Pts',(-19.1090772545539,-21.4858166361586,
16.052080601289));
#156007=CARTESIAN_POINT('Ctrl Pts',(-19.1936338320392,-21.471855975481,
16.0563341791744));
#156008=CARTESIAN_POINT('Ctrl Pts',(-19.2773408795586,-21.453675576209,
16.0605877570599));
#156009=CARTESIAN_POINT('Ctrl Pts',(-19.359425102621,-21.435847639453,16.0647588710378));
#156010=CARTESIAN_POINT('Ctrl Pts',(-19.4406919711073,-21.4139622218931,
16.0689299850158));
#156011=CARTESIAN_POINT('Ctrl Pts',(-19.5207150357481,-21.3881197533225,
16.0731010989937));
#156012=CARTESIAN_POINT('Ctrl Pts',(-19.6007112478768,-21.3622859564417,
16.0772708133141));
#156013=CARTESIAN_POINT('Ctrl Pts',(-19.6794640476569,-21.3324978868904,
16.0814405276345));
#156014=CARTESIAN_POINT('Ctrl Pts',(-19.7565616407639,-21.2989059825307,
16.0856102419549));
#156015=CARTESIAN_POINT('Ctrl Pts',(-19.8336564904078,-21.265315273515,
16.0897798078989));
#156016=CARTESIAN_POINT('Ctrl Pts',(-19.9090958290862,-21.2279211833509,
16.093949373843));
#156017=CARTESIAN_POINT('Ctrl Pts',(-19.9824886317286,-21.1869219530991,
16.0981189397871));
#156018=CARTESIAN_POINT('Ctrl Pts',(-20.0584618347717,-21.14448124049,16.102435102526));
#156019=CARTESIAN_POINT('Ctrl Pts',(-20.1322414512882,-21.0981774147041,
16.1067512652649));
#156020=CARTESIAN_POINT('Ctrl Pts',(-20.203424104004,-21.0482807070076,
16.1110674280038));
#156021=CARTESIAN_POINT('Ctrl Pts',(-20.2722879892948,-21.0000093793159,
16.1152429921955));
#156022=CARTESIAN_POINT('Ctrl Pts',(-20.3387211617825,-20.9483759776501,
16.1194185563872));
#156023=CARTESIAN_POINT('Ctrl Pts',(-20.4023916835437,-20.8936666012171,
16.1235941205789));
#156024=CARTESIAN_POINT('Ctrl Pts',(-20.4692780519966,-20.83619398424,16.1279805825914));
#156025=CARTESIAN_POINT('Ctrl Pts',(-20.5331149297317,-20.7753268941806,
16.1323670446039));
#156026=CARTESIAN_POINT('Ctrl Pts',(-20.5935624370348,-20.7114395535991,
16.1367535066165));
#156027=CARTESIAN_POINT('Ctrl Pts',(-20.6540099443379,-20.6475522130177,
16.141139968629));
#156028=CARTESIAN_POINT('Ctrl Pts',(-20.7110677625944,-20.5806451127527,
16.1455264306415));
#156029=CARTESIAN_POINT('Ctrl Pts',(-20.764447298501,-20.5111291697643,
16.149912892654));
#156030=CARTESIAN_POINT('Ctrl Pts',(-20.8154455601759,-20.4447143500982,
16.1541036735168));
#156031=CARTESIAN_POINT('Ctrl Pts',(-20.8632791399794,-20.3756679864259,
16.1582944543796));
#156032=CARTESIAN_POINT('Ctrl Pts',(-20.9076654294935,-20.3043234082959,
16.1624852352424));
#156033=CARTESIAN_POINT('Ctrl Pts',(-20.9519891627481,-20.233079380358,
16.1666701097864));
#156034=CARTESIAN_POINT('Ctrl Pts',(-20.9928750133147,-20.1595439541276,
16.1708549843304));
#156035=CARTESIAN_POINT('Ctrl Pts',(-21.0300812471761,-20.0840825528053,
16.1750398588744));
#156036=CARTESIAN_POINT('Ctrl Pts',(-21.0672460755937,-20.0087051296902,
16.1792200762261));
#156037=CARTESIAN_POINT('Ctrl Pts',(-21.1007392197538,-19.9314063968234,
16.1834002935778));
#156038=CARTESIAN_POINT('Ctrl Pts',(-21.1303635397436,-19.8525785836825,
16.1875805109294));
#156039=CARTESIAN_POINT('Ctrl Pts',(-21.159964013956,-19.7738142221411,
16.1917573634601));
#156040=CARTESIAN_POINT('Ctrl Pts',(-21.1857016914125,-19.6935236530682,
16.1959342159908));
#156041=CARTESIAN_POINT('Ctrl Pts',(-21.2074270380285,-19.6121202068937,
16.2001110685216));
#156042=CARTESIAN_POINT('Ctrl Pts',(-21.2291418983467,-19.5307560521882,
16.2042859049869));
#156043=CARTESIAN_POINT('Ctrl Pts',(-21.2468481598046,-19.4482805298198,
16.2084607414522));
#156044=CARTESIAN_POINT('Ctrl Pts',(-21.2604461548152,-19.3651220483335,
16.2126355779175));
#156045=CARTESIAN_POINT('Ctrl Pts',(-21.2740449836494,-19.2819584676034,
16.216810670382));
#156046=CARTESIAN_POINT('Ctrl Pts',(-21.2835349604933,-19.1981122945302,
16.2209857628466));
#156047=CARTESIAN_POINT('Ctrl Pts',(-21.2888677421722,-19.1140210480402,
16.2251608553111));
#156048=CARTESIAN_POINT('Ctrl Pts',(-21.2923288662564,-19.0594434830793,
16.2278706067979));
#156049=CARTESIAN_POINT('Ctrl Pts',(-21.2940398771788,-19.0047628516758,
16.2305803582847));
#156050=CARTESIAN_POINT('Ctrl Pts',(-21.293999294499,-18.9500994304893,
16.2332901097715));
#156051=CARTESIAN_POINT('',(-21.2939994369002,-18.9536979607663,16.1667098902285));
#156052=CARTESIAN_POINT('Ctrl Pts',(-17.172599330006,-20.9845253206546,
15.883228700071));
#156053=CARTESIAN_POINT('Ctrl Pts',(-17.2449841511746,-21.0410309575293,
15.8878110784405));
#156054=CARTESIAN_POINT('Ctrl Pts',(-18.0187464880494,-21.577913384796,
15.9347853923704));
#156055=CARTESIAN_POINT('Ctrl Pts',(-20.0538051259393,-21.6762256253679,
16.0241516418607));
#156056=CARTESIAN_POINT('Ctrl Pts',(-21.2452320241039,-20.0081650284355,
16.1140629935438));
#156057=CARTESIAN_POINT('Ctrl Pts',(-21.2975539525536,-19.0564768252052,
16.1615824096664));
#156058=CARTESIAN_POINT('Ctrl Pts',(-21.2967673506771,-18.9536997966296,
16.1667098902285));
#156059=CARTESIAN_POINT('Ctrl Pts',(-21.2939994369002,-18.9536979607663,
16.1667098902285));
#156060=CARTESIAN_POINT('Ctrl Pts',(-21.2940542005915,-18.8711312597184,
16.1708335669039));
#156061=CARTESIAN_POINT('Ctrl Pts',(-21.2901102644712,-18.7884072256502,
16.1749572435793));
#156062=CARTESIAN_POINT('Ctrl Pts',(-21.282148407848,-18.7059518510906,
16.1790809202548));
#156063=CARTESIAN_POINT('Ctrl Pts',(-21.274150019936,-18.6231181475505,
16.1832235175451));
#156064=CARTESIAN_POINT('Ctrl Pts',(-21.2620966823449,-18.5405560554535,
16.1873661148355));
#156065=CARTESIAN_POINT('Ctrl Pts',(-21.2460219433306,-18.45869912201,16.1915087121259));
#156066=CARTESIAN_POINT('Ctrl Pts',(-21.2300543085101,-18.3773875921873,
16.1956237077524));
#156067=CARTESIAN_POINT('Ctrl Pts',(-21.2101187777555,-18.2967723256484,
16.1997387033789));
#156068=CARTESIAN_POINT('Ctrl Pts',(-21.1863001253011,-18.2172727748014,
16.2038536990054));
#156069=CARTESIAN_POINT('Ctrl Pts',(-21.1624916905598,-18.1378073276301,
16.2079669293832));
#156070=CARTESIAN_POINT('Ctrl Pts',(-21.1348035753301,-18.0594570997617,
16.2120801597611));
#156071=CARTESIAN_POINT('Ctrl Pts',(-21.1033710027997,-17.9826285278121,
16.2161933901389));
#156072=CARTESIAN_POINT('Ctrl Pts',(-21.0719418753926,-17.9058083765509,
16.2203061696918));
#156073=CARTESIAN_POINT('Ctrl Pts',(-21.0367692860286,-17.830509988201,
16.2244189492448));
#156074=CARTESIAN_POINT('Ctrl Pts',(-20.998036835518,-17.757120421374,16.2285317287978));
#156075=CARTESIAN_POINT('Ctrl Pts',(-20.9588192445656,-17.68281161896,16.2326960226666));
#156076=CARTESIAN_POINT('Ctrl Pts',(-20.9159522062818,-17.610460238745,
16.2368603165354));
#156077=CARTESIAN_POINT('Ctrl Pts',(-20.8696736494984,-17.5404412648287,
16.2410246104042));
#156078=CARTESIAN_POINT('Ctrl Pts',(-20.8239074514183,-17.4711974842889,
16.2451428005836));
#156079=CARTESIAN_POINT('Ctrl Pts',(-20.7748052350545,-17.4042350697679,
16.2492609907631));
#156080=CARTESIAN_POINT('Ctrl Pts',(-20.7226388747277,-17.3398847975651,
16.2533791809425));
#156081=CARTESIAN_POINT('Ctrl Pts',(-20.6695965003384,-17.2744539105173,
16.257566526656));
#156082=CARTESIAN_POINT('Ctrl Pts',(-20.6133864683218,-17.2117240820488,
16.2617538723695));
#156083=CARTESIAN_POINT('Ctrl Pts',(-20.5543334369044,-17.152003839313,
16.265941218083));
#156084=CARTESIAN_POINT('Ctrl Pts',(-20.495280405487,-17.0922835965773,
16.2701285637965));
#156085=CARTESIAN_POINT('Ctrl Pts',(-20.4333847973435,-17.0355732283015,
16.27431590951));
#156086=CARTESIAN_POINT('Ctrl Pts',(-20.369004471075,-16.9821369642625,
16.2785032552236));
#156087=CARTESIAN_POINT('Ctrl Pts',(-20.3046658312848,-16.9287353003847,
16.2826878896166));
#156088=CARTESIAN_POINT('Ctrl Pts',(-20.2375884427954,-16.8783896656033,
16.2868725240096));
#156089=CARTESIAN_POINT('Ctrl Pts',(-20.1680947292198,-16.8313934104545,
16.2910571584027));
#156090=CARTESIAN_POINT('Ctrl Pts',(-20.0986999313439,-16.7844640486578,
16.2952358364866));
#156091=CARTESIAN_POINT('Ctrl Pts',(-20.0268960178072,-16.740874852386,
16.2994145145706));
#156092=CARTESIAN_POINT('Ctrl Pts',(-19.9530388079927,-16.7008793047445,
16.3035931926545));
#156093=CARTESIAN_POINT('Ctrl Pts',(-19.8778577607726,-16.6601668656558,
16.30784677054));
#156094=CARTESIAN_POINT('Ctrl Pts',(-19.8005494535676,-16.623178482619,
16.3121003484254));
#156095=CARTESIAN_POINT('Ctrl Pts',(-19.7215205448425,-16.5901356572584,
16.3163539263108));
#156096=CARTESIAN_POINT('Ctrl Pts',(-19.6440237657252,-16.5577334315452,
16.3205250402888));
#156097=CARTESIAN_POINT('Ctrl Pts',(-19.5648729481497,-16.5291253296777,
16.3246961542668));
#156098=CARTESIAN_POINT('Ctrl Pts',(-19.4844751811847,-16.5044732887207,
16.3288672682447));
#156099=CARTESIAN_POINT('Ctrl Pts',(-19.4041043924667,-16.479829519994,
16.3330369825651));
#156100=CARTESIAN_POINT('Ctrl Pts',(-19.322487924815,-16.4591393105012,
16.3372066968855));
#156101=CARTESIAN_POINT('Ctrl Pts',(-19.2400494979666,-16.4425152111225,
16.3413764112058));
#156102=CARTESIAN_POINT('Ctrl Pts',(-19.1576140046313,-16.4258917033005,
16.3455459771499));
#156103=CARTESIAN_POINT('Ctrl Pts',(-19.0743570613773,-16.4133341080143,
16.3497155430939));
#156104=CARTESIAN_POINT('Ctrl Pts',(-18.9907127437434,-16.4049038951779,
16.353885109038));
#156105=CARTESIAN_POINT('Ctrl Pts',(-18.9041275950881,-16.396177286458,
16.3582012717769));
#156106=CARTESIAN_POINT('Ctrl Pts',(-18.8171278498229,-16.3918737507556,
16.3625174345158));
#156107=CARTESIAN_POINT('Ctrl Pts',(-18.7301989430813,-16.3920028218831,
16.3668335972547));
#156108=CARTESIAN_POINT('Ctrl Pts',(-18.6461017363336,-16.3921276885323,
16.3710091614464));
#156109=CARTESIAN_POINT('Ctrl Pts',(-18.5620712918894,-16.3964007414036,
16.3751847256381));
#156110=CARTESIAN_POINT('Ctrl Pts',(-18.4785435740566,-16.4047775883437,
16.3793602898298));
#156111=CARTESIAN_POINT('Ctrl Pts',(-18.3907970697643,-16.4135775299086,
16.3837467518423));
#156112=CARTESIAN_POINT('Ctrl Pts',(-18.3036059893689,-16.42690663756,16.3881332138549));
#156113=CARTESIAN_POINT('Ctrl Pts',(-18.2174632822103,-16.4446528323395,
16.3925196758674));
#156114=CARTESIAN_POINT('Ctrl Pts',(-18.1313205750517,-16.4623990271191,
16.3969061378799));
#156115=CARTESIAN_POINT('Ctrl Pts',(-18.0462267834429,-16.4845620891763,
16.4012925998925));
#156116=CARTESIAN_POINT('Ctrl Pts',(-17.9626538344087,-16.510970485056,
16.405679061905));
#156117=CARTESIAN_POINT('Ctrl Pts',(-17.8829262006443,-16.5361637914947,
16.4098636962981));
#156118=CARTESIAN_POINT('Ctrl Pts',(-17.8042857709966,-16.5653141227608,
16.4140483306911));
#156119=CARTESIAN_POINT('Ctrl Pts',(-17.7271537286292,-16.5983091567016,
16.4182329650842));
#156120=CARTESIAN_POINT('Ctrl Pts',(-17.6501314741771,-16.6312572262956,
16.4224116431681));
#156121=CARTESIAN_POINT('Ctrl Pts',(-17.5746137617239,-16.6680389491568,
16.426590321252));
#156122=CARTESIAN_POINT('Ctrl Pts',(-17.5010063287304,-16.708492343091,
16.430768999336));
#156123=CARTESIAN_POINT('Ctrl Pts',(-17.4260795354011,-16.7496708350382,
16.4350225772214));
#156124=CARTESIAN_POINT('Ctrl Pts',(-17.3531326383836,-16.7946537768951,
16.4392761551069));
#156125=CARTESIAN_POINT('Ctrl Pts',(-17.2825720020047,-16.8432191278762,
16.4435297329923));
#156126=CARTESIAN_POINT('Ctrl Pts',(-17.2133793212498,-16.8908429447609,
16.4477008469703));
#156127=CARTESIAN_POINT('Ctrl Pts',(-17.1464815985698,-16.9419112335081,
16.4518719609482));
#156128=CARTESIAN_POINT('Ctrl Pts',(-17.082235347001,-16.9961693500962,
16.4560430749262));
#156129=CARTESIAN_POINT('Ctrl Pts',(-17.0180106538824,-17.0504092598493,
16.4602127892466));
#156130=CARTESIAN_POINT('Ctrl Pts',(-16.9564360160344,-17.1078365750808,
16.4643825035669));
#156131=CARTESIAN_POINT('Ctrl Pts',(-16.897835422393,-17.1681559362037,
16.4685522178873));
#156132=CARTESIAN_POINT('Ctrl Pts',(-16.8392369140123,-17.2284731509048,
16.4727217838314));
#156133=CARTESIAN_POINT('Ctrl Pts',(-16.7836125593685,-17.2916818763298,
16.4768913497754));
#156134=CARTESIAN_POINT('Ctrl Pts',(-16.731249001788,-17.3574503961429,
16.4810609157195));
#156135=CARTESIAN_POINT('Ctrl Pts',(-16.6770444061204,-17.4255312559784,
16.4853770784584));
#156136=CARTESIAN_POINT('Ctrl Pts',(-16.6263345016126,-17.4963548514855,
16.4896932411973));
#156137=CARTESIAN_POINT('Ctrl Pts',(-16.5793900615229,-17.5695181690106,
16.4940094039362));
#156138=CARTESIAN_POINT('Ctrl Pts',(-16.5339748316314,-17.6402981991629,
16.4981849681279));
#156139=CARTESIAN_POINT('Ctrl Pts',(-16.4920837070567,-17.7132674273088,
16.5023605323196));
#156140=CARTESIAN_POINT('Ctrl Pts',(-16.453915340234,-17.7880352478275,
16.5065360965113));
#156141=CARTESIAN_POINT('Ctrl Pts',(-16.41381917994,-17.8665794132169,16.5109225585238));
#156142=CARTESIAN_POINT('Ctrl Pts',(-16.3778319719893,-17.9471081067069,
16.5153090205363));
#156143=CARTESIAN_POINT('Ctrl Pts',(-16.3461262998435,-18.0291461696993,
16.5196954825489));
#156144=CARTESIAN_POINT('Ctrl Pts',(-16.3144206276976,-18.1111842326916,
16.5240819445614));
#156145=CARTESIAN_POINT('Ctrl Pts',(-16.2869966000408,-18.1947310901858,
16.5284684065739));
#156146=CARTESIAN_POINT('Ctrl Pts',(-16.2639654295305,-18.2792970784325,
16.5328548685865));
#156147=CARTESIAN_POINT('Ctrl Pts',(-16.2419939573157,-18.3599720602031,
16.5370395029795));
#156148=CARTESIAN_POINT('Ctrl Pts',(-16.223938199736,-18.4418747378536,
16.5412241373726));
#156149=CARTESIAN_POINT('Ctrl Pts',(-16.2099316900943,-18.5245901651461,
16.5454087717656));
#156150=CARTESIAN_POINT('Ctrl Pts',(-16.1959451169854,-18.607187857266,
16.5495874498496));
#156151=CARTESIAN_POINT('Ctrl Pts',(-16.1859964196337,-18.6905955514663,
16.5537661279335));
#156152=CARTESIAN_POINT('Ctrl Pts',(-16.18016901464,-18.7743844088623,16.5579448060175));
#156153=CARTESIAN_POINT('Ctrl Pts',(-16.1742371575999,-18.8596751213092,
16.5621983839029));
#156154=CARTESIAN_POINT('Ctrl Pts',(-16.1725759211884,-18.9453603308624,
16.5664519617883));
#156155=CARTESIAN_POINT('Ctrl Pts',(-16.1752185615464,-19.0309781629655,
16.5707055396738));
#156156=CARTESIAN_POINT('Ctrl Pts',(-16.1778099691644,-19.1149361263239,
16.5748766536517));
#156157=CARTESIAN_POINT('Ctrl Pts',(-16.1845398497979,-19.1988288204158,
16.5790477676297));
#156158=CARTESIAN_POINT('Ctrl Pts',(-16.1953870618677,-19.2822186402179,
16.5832188816076));
#156159=CARTESIAN_POINT('Ctrl Pts',(-16.2062306340508,-19.3655804777606,
16.587388595928));
#156160=CARTESIAN_POINT('Ctrl Pts',(-16.221188734479,-19.4484393203326,
16.5915583102484));
#156161=CARTESIAN_POINT('Ctrl Pts',(-16.2401883815476,-19.5303628719685,
16.5957280245687));
#156162=CARTESIAN_POINT('Ctrl Pts',(-16.2591873525271,-19.6122835084129,
16.5998975905128));
#156163=CARTESIAN_POINT('Ctrl Pts',(-16.2822274794425,-19.6932684721474,
16.6040671564568));
#156164=CARTESIAN_POINT('Ctrl Pts',(-16.3091849959464,-19.7728971897362,
16.6082367224009));
#156165=CARTESIAN_POINT('Ctrl Pts',(-16.337090305475,-19.8553255548027,
16.6125528851398));
#156166=CARTESIAN_POINT('Ctrl Pts',(-16.3691934316988,-19.9363000284497,
16.6168690478787));
#156167=CARTESIAN_POINT('Ctrl Pts',(-16.4053020683426,-20.0153747895708,
16.6211852106176));
#156168=CARTESIAN_POINT('Ctrl Pts',(-16.4402344699458,-20.0918736986655,
16.6253607748093));
#156169=CARTESIAN_POINT('Ctrl Pts',(-16.4789151719814,-20.1665943642432,
16.629536339001));
#156170=CARTESIAN_POINT('Ctrl Pts',(-16.5211232637327,-20.2391583236289,
16.6337119031927));
#156171=CARTESIAN_POINT('Ctrl Pts',(-16.5654631858582,-20.3153873160987,
16.6380983652052));
#156172=CARTESIAN_POINT('Ctrl Pts',(-16.613695880029,-20.3892355173248,
16.6424848272177));
#156173=CARTESIAN_POINT('Ctrl Pts',(-16.6655152292138,-20.460300617591,
16.6468712892303));
#156174=CARTESIAN_POINT('Ctrl Pts',(-16.7173345783985,-20.5313657178572,
16.6512577512428));
#156175=CARTESIAN_POINT('Ctrl Pts',(-16.7727401579416,-20.5996473145404,
16.6556442132554));
#156176=CARTESIAN_POINT('Ctrl Pts',(-16.8313804354228,-20.664786849695,
16.6600306752679));
#156177=CARTESIAN_POINT('Ctrl Pts',(-16.8873083679682,-20.7269134235218,
16.6642142460504));
#156178=CARTESIAN_POINT('Ctrl Pts',(-16.9463864967696,-20.7864133665619,
16.668397816833));
#156179=CARTESIAN_POINT('Ctrl Pts',(-17.0083384129404,-20.8429500487709,
16.6725813876155));
#156180=CARTESIAN_POINT('Ctrl Pts',(-17.0616528481945,-20.8916042546362,
16.6761816751837));
#156181=CARTESIAN_POINT('Ctrl Pts',(-17.1170947828409,-20.9380641965746,
16.679781962752));
#156182=CARTESIAN_POINT('Ctrl Pts',(-17.1744641402401,-20.9821349467765,
16.6833822503202));
#156183=CARTESIAN_POINT('Origin',(-18.734,-18.952,-1.76670989022851));
#156184=CARTESIAN_POINT('',(-17.1718942801479,-20.9854857634355,17.5498940685532));
#156185=CARTESIAN_POINT('',(-17.1769969312964,-20.9788274605145,17.483325298233));
#156186=CARTESIAN_POINT('',(-17.1744641402401,-20.9821349467765,-1.76670989022851));
#156187=CARTESIAN_POINT('',(-21.2942629985695,-18.9511644346814,17.0332901097715));
#156188=CARTESIAN_POINT('Ctrl Pts',(-21.2979001731334,-18.9511632476561,
17.0332901097715));
#156189=CARTESIAN_POINT('Ctrl Pts',(-21.2980948808476,-18.9054257555603,
17.0355745863224));
#156190=CARTESIAN_POINT('Ctrl Pts',(-21.2762380388006,-18.0111494605167,
17.0802509984337));
#156191=CARTESIAN_POINT('Ctrl Pts',(-20.2331955662249,-16.3222274596702,
17.1673193461055));
#156192=CARTESIAN_POINT('Ctrl Pts',(-17.3342635896144,-16.2679677831473,
17.2944951527869));
#156193=CARTESIAN_POINT('Ctrl Pts',(-15.7195028920934,-18.6761410757601,
17.4216709594684));
#156194=CARTESIAN_POINT('Ctrl Pts',(-16.4898975455887,-20.4576174486145,
17.5068039313905));
#156195=CARTESIAN_POINT('Ctrl Pts',(-17.1663500614582,-20.9812337393009,
17.5495449677521));
#156196=CARTESIAN_POINT('Ctrl Pts',(-17.1718942801479,-20.9854857634355,
17.5498940685532));
#156197=CARTESIAN_POINT('Ctrl Pts',(-17.1744641402402,-20.9821349467765,
16.7498176584939));
#156198=CARTESIAN_POINT('Ctrl Pts',(-17.2411413997508,-21.03335596408,16.7539938117457));
#156199=CARTESIAN_POINT('Ctrl Pts',(-17.3102910949476,-21.0812474621041,
16.7581699649975));
#156200=CARTESIAN_POINT('Ctrl Pts',(-17.3815399059492,-21.1255803859071,
16.7623461182494));
#156201=CARTESIAN_POINT('Ctrl Pts',(-17.452915090555,-21.1699919427608,
16.7665296787201));
#156202=CARTESIAN_POINT('Ctrl Pts',(-17.5263964265398,-21.2108320914119,
16.7707132391908));
#156203=CARTESIAN_POINT('Ctrl Pts',(-17.6015859266022,-21.2479177612386,
16.7748967996615));
#156204=CARTESIAN_POINT('Ctrl Pts',(-17.6668572118987,-21.2801114762341,
16.7785285084614));
#156205=CARTESIAN_POINT('Ctrl Pts',(-17.7334152100966,-21.3094765764609,
16.7821602172613));
#156206=CARTESIAN_POINT('Ctrl Pts',(-17.8009895271371,-21.3359235427186,
16.7857919260613));
#156207=CARTESIAN_POINT('Ctrl Pts',(-17.8788519954,-21.3663970445028,16.7899765604543));
#156208=CARTESIAN_POINT('Ctrl Pts',(-17.9583538968788,-21.3931085897472,
16.7941611948473));
#156209=CARTESIAN_POINT('Ctrl Pts',(-18.0390969463692,-21.4158810332592,
16.7983458292404));
#156210=CARTESIAN_POINT('Ctrl Pts',(-18.1197250681227,-21.4386210630166,
16.8025245073243));
#156211=CARTESIAN_POINT('Ctrl Pts',(-18.2015903898501,-21.4574330041517,
16.8067031854083));
#156212=CARTESIAN_POINT('Ctrl Pts',(-18.2842754534887,-21.4721880549406,
16.8108818634922));
#156213=CARTESIAN_POINT('Ctrl Pts',(-18.3684425874682,-21.4872075794106,
16.8151354413777));
#156214=CARTESIAN_POINT('Ctrl Pts',(-18.4534586911853,-21.49802316776,16.8193890192631));
#156215=CARTESIAN_POINT('Ctrl Pts',(-18.538868095807,-21.5045523579284,
16.8236425971485));
#156216=CARTESIAN_POINT('Ctrl Pts',(-18.6226216724574,-21.5109549670048,
16.8278137111265));
#156217=CARTESIAN_POINT('Ctrl Pts',(-18.7067529564692,-21.5132358584627,
16.8319848251044));
#156218=CARTESIAN_POINT('Ctrl Pts',(-18.7908245916082,-21.5113692515517,
16.8361559390824));
#156219=CARTESIAN_POINT('Ctrl Pts',(-18.8748680156982,-21.5095032709988,
16.8403256534027));
#156220=CARTESIAN_POINT('Ctrl Pts',(-18.9588513711302,-21.503492566284,
16.8444953677231));
#156221=CARTESIAN_POINT('Ctrl Pts',(-19.0423370360803,-21.4933634671533,
16.8486650820435));
#156222=CARTESIAN_POINT('Ctrl Pts',(-19.1258197302523,-21.4832347284594,
16.8528346479875));
#156223=CARTESIAN_POINT('Ctrl Pts',(-19.2088043125732,-21.4689879429832,
16.8570042139316));
#156224=CARTESIAN_POINT('Ctrl Pts',(-19.2908593851775,-21.4507011876452,
16.8611737798756));
#156225=CARTESIAN_POINT('Ctrl Pts',(-19.3757994129086,-21.4317714925488,
16.8654899426145));
#156226=CARTESIAN_POINT('Ctrl Pts',(-19.4597428368621,-21.4085125658604,
16.8698061053535));
#156227=CARTESIAN_POINT('Ctrl Pts',(-19.5422258260852,-21.381067931131,
16.8741222680924));
#156228=CARTESIAN_POINT('Ctrl Pts',(-19.6220219406102,-21.3545173024912,
16.8782978322841));
#156229=CARTESIAN_POINT('Ctrl Pts',(-19.7004508845915,-21.3240496914869,
16.8824733964757));
#156230=CARTESIAN_POINT('Ctrl Pts',(-19.7771127399862,-21.2898442659165,
16.8866489606674));
#156231=CARTESIAN_POINT('Ctrl Pts',(-19.8576466034505,-21.2539112056161,
16.8910354226799));
#156232=CARTESIAN_POINT('Ctrl Pts',(-19.9362296554817,-21.2138530785412,
16.8954218846925));
#156233=CARTESIAN_POINT('Ctrl Pts',(-20.0124291551049,-21.169931219713,
16.899808346705));
#156234=CARTESIAN_POINT('Ctrl Pts',(-20.0886286547281,-21.1260093608849,
16.9041948087175));
#156235=CARTESIAN_POINT('Ctrl Pts',(-20.1624441562134,-21.0782241494638,
16.9085812707301));
#156236=CARTESIAN_POINT('Ctrl Pts',(-20.2334815623277,-21.0268867545577,
16.9129677327426));
#156237=CARTESIAN_POINT('Ctrl Pts',(-20.3007008312569,-20.9783086554537,
16.9171184300413));
#156238=CARTESIAN_POINT('Ctrl Pts',(-20.3656920487852,-20.9263629083339,
16.9212691273401));
#156239=CARTESIAN_POINT('Ctrl Pts',(-20.4280939407346,-20.8712826055499,
16.9254198246388));
#156240=CARTESIAN_POINT('Ctrl Pts',(-20.4904067758306,-20.816280910614,
16.9295645982704));
#156241=CARTESIAN_POINT('Ctrl Pts',(-20.5501372744547,-20.758153849065,
16.9337093719019));
#156242=CARTESIAN_POINT('Ctrl Pts',(-20.6069541187602,-20.6971770308536,
16.9378541455334));
#156243=CARTESIAN_POINT('Ctrl Pts',(-20.6637057912846,-20.636270156123,
16.9419941649009));
#156244=CARTESIAN_POINT('Ctrl Pts',(-20.7175501324576,-20.5725203603438,
16.9461341842684));
#156245=CARTESIAN_POINT('Ctrl Pts',(-20.7681909845743,-20.5062416280221,
16.9502742036359));
#156246=CARTESIAN_POINT('Ctrl Pts',(-20.8188004163148,-20.4400040186795,
16.9544116543072));
#156247=CARTESIAN_POINT('Ctrl Pts',(-20.8662100198436,-20.3712409577298,
16.9585491049784));
#156248=CARTESIAN_POINT('Ctrl Pts',(-20.9101632231194,-20.3003002730633,
16.9626865556497));
#156249=CARTESIAN_POINT('Ctrl Pts',(-20.9541028768145,-20.2293814574863,
16.9668227308571));
#156250=CARTESIAN_POINT('Ctrl Pts',(-20.9945879994369,-20.1562867489274,
16.9709589060645));
#156251=CARTESIAN_POINT('Ctrl Pts',(-21.0314055962389,-20.0813925475095,
16.9750950812719));
#156252=CARTESIAN_POINT('Ctrl Pts',(-21.0682233367814,-20.0064980536955,
16.9792312726275));
#156253=CARTESIAN_POINT('Ctrl Pts',(-21.101373318238,-19.9298044742117,
16.983367463983));
#156254=CARTESIAN_POINT('Ctrl Pts',(-21.1306893947114,-19.8517110343203,
16.9875036553386));
#156255=CARTESIAN_POINT('Ctrl Pts',(-21.1600333335746,-19.773543373383,
16.9916437777855));
#156256=CARTESIAN_POINT('Ctrl Pts',(-21.1855359272153,-19.6939736349119,
16.9957839002324));
#156257=CARTESIAN_POINT('Ctrl Pts',(-21.2070801670876,-19.6134185415892,
16.9999240226793));
#156258=CARTESIAN_POINT('Ctrl Pts',(-21.2286351815299,-19.5328231615589,
17.0040662156583));
#156259=CARTESIAN_POINT('Ctrl Pts',(-21.2462278030767,-19.4512419037244,
17.0082084086373));
#156260=CARTESIAN_POINT('Ctrl Pts',(-21.2597921942375,-19.3691016561091,
17.0123506016163));
#156261=CARTESIAN_POINT('Ctrl Pts',(-21.2733789861849,-19.286825758752,
17.016499635181));
#156262=CARTESIAN_POINT('Ctrl Pts',(-21.2829242114339,-19.2039894937101,
17.0206486687457));
#156263=CARTESIAN_POINT('Ctrl Pts',(-21.2884139728529,-19.1210244221818,
17.0247977023105));
#156264=CARTESIAN_POINT('Ctrl Pts',(-21.2921595270972,-19.0644190158498,
17.0276285047975));
#156265=CARTESIAN_POINT('Ctrl Pts',(-21.2940183320645,-19.0077536994293,
17.0304593072845));
#156266=CARTESIAN_POINT('Ctrl Pts',(-21.2939998636668,-18.9511645205579,
17.0332901097715));
#156267=CARTESIAN_POINT('',(-21.2938494935628,-18.9531967451209,16.9667098397524));
#156268=CARTESIAN_POINT('Ctrl Pts',(-17.1744641402401,-20.9821349467765,
16.6833822503202));
#156269=CARTESIAN_POINT('Ctrl Pts',(-17.2433976321044,-21.0350891864301,
16.6877082599714));
#156270=CARTESIAN_POINT('Ctrl Pts',(-17.3151146538089,-21.0845925459325,
16.6920342696226));
#156271=CARTESIAN_POINT('Ctrl Pts',(-17.3892303913309,-21.1303467813,16.6963602792738));
#156272=CARTESIAN_POINT('Ctrl Pts',(-17.4606967411856,-21.1744654570554,
16.7005316486691));
#156273=CARTESIAN_POINT('Ctrl Pts',(-17.5343928021794,-21.2150982250402,
16.7047030180644));
#156274=CARTESIAN_POINT('Ctrl Pts',(-17.6099424306077,-21.2520205609281,
16.7088743874597));
#156275=CARTESIAN_POINT('Ctrl Pts',(-17.6854639536298,-21.2889291612454,
16.7130442050534));
#156276=CARTESIAN_POINT('Ctrl Pts',(-17.7628372618191,-21.3221298688539,
16.7172140226471));
#156277=CARTESIAN_POINT('Ctrl Pts',(-17.8416619148195,-21.3514442568512,
16.7213838402409));
#156278=CARTESIAN_POINT('Ctrl Pts',(-17.9204808895674,-21.3807565331426,
16.7255533574555));
#156279=CARTESIAN_POINT('Ctrl Pts',(-18.0007505699482,-21.4061828864854,
16.7297228746702));
#156280=CARTESIAN_POINT('Ctrl Pts',(-18.0820521418072,-21.4275936641941,
16.7338923918848));
#156281=CARTESIAN_POINT('Ctrl Pts',(-18.163372245078,-21.4490093221521,
16.7380628594752));
#156282=CARTESIAN_POINT('Ctrl Pts',(-18.2457242617706,-21.4664074711392,
16.7422333270656));
#156283=CARTESIAN_POINT('Ctrl Pts',(-18.3286772203917,-21.4797091296925,
16.746403794656));
#156284=CARTESIAN_POINT('Ctrl Pts',(-18.4117242396608,-21.4930258710425,
16.750578991154));
#156285=CARTESIAN_POINT('Ctrl Pts',(-18.4953731056364,-21.5022367814287,
16.7547541876521));
#156286=CARTESIAN_POINT('Ctrl Pts',(-18.5791863014753,-21.5073146026955,
16.7589293841502));
#156287=CARTESIAN_POINT('Ctrl Pts',(-18.6630562519229,-21.5123958624395,
16.7631074079076));
#156288=CARTESIAN_POINT('Ctrl Pts',(-18.7470902943607,-21.5133384585987,
16.767285431665));
#156289=CARTESIAN_POINT('Ctrl Pts',(-18.8308518534922,-21.5101672577209,
16.7714634554225));
#156290=CARTESIAN_POINT('Ctrl Pts',(-18.914746487242,-21.5069910186567,
16.7756481169374));
#156291=CARTESIAN_POINT('Ctrl Pts',(-18.9983673171488,-21.4996879836572,
16.7798327784523));
#156292=CARTESIAN_POINT('Ctrl Pts',(-19.0812844001845,-21.4883346674657,
16.7840174399673));
#156293=CARTESIAN_POINT('Ctrl Pts',(-19.1023475182635,-21.4854506267979,
16.7850804539613));
#156294=CARTESIAN_POINT('Ctrl Pts',(-19.12336528706,-21.4823054789026,16.7861434679553));
#156295=CARTESIAN_POINT('Ctrl Pts',(-19.1443308019265,-21.4789009939035,
16.7872064819493));
#156296=CARTESIAN_POINT('Ctrl Pts',(-19.226863125181,-21.4654989831134,
16.7913911163424));
#156297=CARTESIAN_POINT('Ctrl Pts',(-19.3088917529366,-21.4480243381486,
16.7955757507354));
#156298=CARTESIAN_POINT('Ctrl Pts',(-19.3899836880773,-21.4265273085938,
16.7997603851285));
#156299=CARTESIAN_POINT('Ctrl Pts',(-19.4709601988853,-21.4050608773999,
16.8039390632124));
#156300=CARTESIAN_POINT('Ctrl Pts',(-19.5510022244941,-21.3795835508679,
16.8081177412964));
#156301=CARTESIAN_POINT('Ctrl Pts',(-19.6296848716226,-21.3501969499494,
16.8122964193803));
#156302=CARTESIAN_POINT('Ctrl Pts',(-19.7097778486527,-21.3202836153291,
16.8165499972657));
#156303=CARTESIAN_POINT('Ctrl Pts',(-19.7884617582359,-21.2863195576314,
16.8208035751512));
#156304=CARTESIAN_POINT('Ctrl Pts',(-19.8653024038482,-21.2484657347862,
16.8250571530366));
#156305=CARTESIAN_POINT('Ctrl Pts',(-19.9406533436032,-21.2113457821626,
16.8292282670146));
#156306=CARTESIAN_POINT('Ctrl Pts',(-20.0142314204538,-21.1704857525211,
16.8333993809925));
#156307=CARTESIAN_POINT('Ctrl Pts',(-20.0856470518143,-21.1260860717372,
16.8375704949705));
#156308=CARTESIAN_POINT('Ctrl Pts',(-20.15703871897,-21.081701289695,16.8417402092909));
#156309=CARTESIAN_POINT('Ctrl Pts',(-20.2262689913883,-21.0337794581181,
16.8459099236112));
#156310=CARTESIAN_POINT('Ctrl Pts',(-20.2929745824341,-20.9825659928514,
16.8500796379316));
#156311=CARTESIAN_POINT('Ctrl Pts',(-20.3596777998085,-20.9313543499797,
16.8542492038756));
#156312=CARTESIAN_POINT('Ctrl Pts',(-20.4238561500589,-20.8768515871279,
16.8584187698197));
#156313=CARTESIAN_POINT('Ctrl Pts',(-20.4851780435301,-20.8193444941569,
16.8625883357637));
#156314=CARTESIAN_POINT('Ctrl Pts',(-20.5486559391271,-20.7598155227396,
16.8669044985026));
#156315=CARTESIAN_POINT('Ctrl Pts',(-20.6090723898813,-20.6970673867193,
16.8712206612416));
#156316=CARTESIAN_POINT('Ctrl Pts',(-20.6661012016726,-20.6314597186284,
16.8755368239805));
#156317=CARTESIAN_POINT('Ctrl Pts',(-20.7212723059182,-20.5679892134248,
16.8797123881722));
#156318=CARTESIAN_POINT('Ctrl Pts',(-20.7732728325614,-20.5018430132074,
16.8838879523639));
#156319=CARTESIAN_POINT('Ctrl Pts',(-20.8218497444837,-20.4333788996943,
16.8880635165556));
#156320=CARTESIAN_POINT('Ctrl Pts',(-20.8728801607464,-20.3614568265657,
16.8924499785681));
#156321=CARTESIAN_POINT('Ctrl Pts',(-20.9201317067406,-20.2869770238507,
16.8968364405806));
#156322=CARTESIAN_POINT('Ctrl Pts',(-20.9633649162028,-20.2103847068381,
16.9012229025932));
#156323=CARTESIAN_POINT('Ctrl Pts',(-21.0065981256651,-20.1337923898255,
16.9056093646057));
#156324=CARTESIAN_POINT('Ctrl Pts',(-21.0458128079223,-20.0550881117615,
16.9099958266183));
#156325=CARTESIAN_POINT('Ctrl Pts',(-21.0808281256648,-19.9747403133684,
16.9143822886308));
#156326=CARTESIAN_POINT('Ctrl Pts',(-21.1176528956138,-19.890240460661,
16.9189954255354));
#156327=CARTESIAN_POINT('Ctrl Pts',(-21.1499518315865,-19.8036540013275,
16.9236085624399));
#156328=CARTESIAN_POINT('Ctrl Pts',(-21.1775079602931,-19.7154584782318,
16.9282216993445));
#156329=CARTESIAN_POINT('Ctrl Pts',(-21.2049852187145,-19.6275153855896,
16.9328216326736));
#156330=CARTESIAN_POINT('Ctrl Pts',(-21.2277466226989,-19.5379726851093,
16.9374215660027));
#156331=CARTESIAN_POINT('Ctrl Pts',(-21.2456232056933,-19.4473270360306,
16.9420214993319));
#156332=CARTESIAN_POINT('Ctrl Pts',(-21.2634117418665,-19.3571278403517,
16.9465987767929));
#156333=CARTESIAN_POINT('Ctrl Pts',(-21.2763633328304,-19.2658368103367,
16.9511760542538));
#156334=CARTESIAN_POINT('Ctrl Pts',(-21.2843593339855,-19.1739623111095,
16.9557533317148));
#156335=CARTESIAN_POINT('Ctrl Pts',(-21.2907392715843,-19.1006564722762,
16.9594055003435));
#156336=CARTESIAN_POINT('Ctrl Pts',(-21.2939652250916,-19.0269796001108,
16.9630576689721));
#156337=CARTESIAN_POINT('Ctrl Pts',(-21.2939997202205,-18.9531968587605,
16.9667098376008));
#156338=CARTESIAN_POINT('Ctrl Pts',(-21.290325207156,-18.9531940791588,
16.9667098902285));
#156339=CARTESIAN_POINT('Ctrl Pts',(-21.2882101978943,-18.4498774972589,
16.9916592919231));
#156340=CARTESIAN_POINT('Ctrl Pts',(-20.9008594754591,-17.088363994255,
17.0590006291781));
#156341=CARTESIAN_POINT('Ctrl Pts',(-18.6858816908488,-15.9252896642242,
17.1687339019936));
#156342=CARTESIAN_POINT('Ctrl Pts',(-16.1629700668002,-17.3541589844551,
17.2959097086751));
#156343=CARTESIAN_POINT('Ctrl Pts',(-16.0276178903722,-19.7410799583894,
17.4007735074215));
#156344=CARTESIAN_POINT('Ctrl Pts',(-16.8552506915702,-20.7323953231713,
17.4632453706075));
#156345=CARTESIAN_POINT('Ctrl Pts',(-17.1769969312964,-20.9788274605145,
17.483325298233));
#156346=CARTESIAN_POINT('Origin',(-18.734,-18.952,-1.76670989022851));
#156347=CARTESIAN_POINT('',(-17.1744641402401,-20.9821349467765,18.3499540410247));
#156348=CARTESIAN_POINT('',(-17.1744641402402,-20.9821349467765,18.2832318482317));
#156349=CARTESIAN_POINT('',(-17.1744641402401,-20.9821349467765,-1.76670989022851));
#156350=CARTESIAN_POINT('',(-21.2939989159607,-18.9543559031924,17.8332901097715));
#156351=CARTESIAN_POINT('Ctrl Pts',(-21.2939989159607,-18.9543559031924,
17.8332901097715));
#156352=CARTESIAN_POINT('Ctrl Pts',(-21.2940751741219,-18.8714913735434,
17.837412174938));
#156353=CARTESIAN_POINT('Ctrl Pts',(-21.290123839502,-18.7885152466555,
17.8415342401044));
#156354=CARTESIAN_POINT('Ctrl Pts',(-21.2821391268744,-18.7058557534859,
17.8456563052709));
#156355=CARTESIAN_POINT('Ctrl Pts',(-21.2741597741335,-18.6232517470386,
17.8497756034244));
#156356=CARTESIAN_POINT('Ctrl Pts',(-21.262152459652,-18.5409644216312,
17.8538949015779));
#156357=CARTESIAN_POINT('Ctrl Pts',(-21.2461634417033,-18.4594202174576,
17.8580141997315));
#156358=CARTESIAN_POINT('Ctrl Pts',(-21.2301800733889,-18.3779048264943,
17.862132042353));
#156359=CARTESIAN_POINT('Ctrl Pts',(-21.2102178848107,-18.2971324990613,
17.8662498849744));
#156360=CARTESIAN_POINT('Ctrl Pts',(-21.1863745538874,-18.217521240984,
17.8703677275959));
#156361=CARTESIAN_POINT('Ctrl Pts',(-21.1625320679642,-18.1379128043046,
17.8744854242823));
#156362=CARTESIAN_POINT('Ctrl Pts',(-21.1348088500427,-18.0594658076282,
17.8786031209688));
#156363=CARTESIAN_POINT('Ctrl Pts',(-21.103352505349,-17.9825833169393,
17.8827208176552));
#156364=CARTESIAN_POINT('Ctrl Pts',(-21.071866121991,-17.905627408714,17.8868424464612));
#156365=CARTESIAN_POINT('Ctrl Pts',(-21.0366396717683,-17.8302394286303,
17.8909640752672));
#156366=CARTESIAN_POINT('Ctrl Pts',(-20.9978687619911,-17.7568020128526,
17.8950857040732));
#156367=CARTESIAN_POINT('Ctrl Pts',(-20.9590794967265,-17.683329829267,
17.8992092842005));
#156368=CARTESIAN_POINT('Ctrl Pts',(-20.9167426732498,-17.6118104548626,
17.9033328643279));
#156369=CARTESIAN_POINT('Ctrl Pts',(-20.8710983794442,-17.5425992349311,
17.9074564444553));
#156370=CARTESIAN_POINT('Ctrl Pts',(-20.8253741239691,-17.4732667677585,
17.9115872484506));
#156371=CARTESIAN_POINT('Ctrl Pts',(-20.776331105883,-17.4062509123682,
17.9157180524459));
#156372=CARTESIAN_POINT('Ctrl Pts',(-20.724250792007,-17.3418752269108,
17.9198488564413));
#156373=CARTESIAN_POINT('Ctrl Pts',(-20.6800170723894,-17.2871985975131,
17.9233572996922));
#156374=CARTESIAN_POINT('Ctrl Pts',(-20.6335931281536,-17.2344260450368,
17.9268657429431));
#156375=CARTESIAN_POINT('Ctrl Pts',(-20.5851713910723,-17.1837340469049,
17.930374186194));
#156376=CARTESIAN_POINT('Ctrl Pts',(-20.5274172101246,-17.1232720517519,
17.934558820587));
#156377=CARTESIAN_POINT('Ctrl Pts',(-20.4665902688467,-17.0655300202436,
17.93874345498));
#156378=CARTESIAN_POINT('Ctrl Pts',(-20.4029770272299,-17.0108365131759,
17.942928089373));
#156379=CARTESIAN_POINT('Ctrl Pts',(-20.3394543311886,-16.9562208555457,
17.9471067674569));
#156380=CARTESIAN_POINT('Ctrl Pts',(-20.2731535582845,-16.9046454006956,
17.9512854455408));
#156381=CARTESIAN_POINT('Ctrl Pts',(-20.2043989371765,-16.8564029572577,
17.9554641236247));
#156382=CARTESIAN_POINT('Ctrl Pts',(-20.1344119388971,-16.8072958026916,
17.9597177015102));
#156383=CARTESIAN_POINT('Ctrl Pts',(-20.0618825897098,-16.7616426719214,
17.9639712793956));
#156384=CARTESIAN_POINT('Ctrl Pts',(-19.9871893049686,-16.7197104654834,
17.9682248572811));
#156385=CARTESIAN_POINT('Ctrl Pts',(-19.9139440953053,-16.6785911966919,
17.972395971259));
#156386=CARTESIAN_POINT('Ctrl Pts',(-19.8386185251851,-16.6410501005271,
17.9765670852369));
#156387=CARTESIAN_POINT('Ctrl Pts',(-19.7615983036833,-16.6072949596448,
17.9807381992148));
#156388=CARTESIAN_POINT('Ctrl Pts',(-19.6846039270607,-16.573551145626,
17.9849079135351));
#156389=CARTESIAN_POINT('Ctrl Pts',(-19.6059164494111,-16.5435909483338,
17.9890776278554));
#156390=CARTESIAN_POINT('Ctrl Pts',(-19.5259437923517,-16.5175750104479,
17.9932473421758));
#156391=CARTESIAN_POINT('Ctrl Pts',(-19.4459739810627,-16.4915599983208,
17.9974169081197));
#156392=CARTESIAN_POINT('Ctrl Pts',(-19.3647195190219,-16.4694891080429,
18.0015864740637));
#156393=CARTESIAN_POINT('Ctrl Pts',(-19.2826045027052,-16.4514734355317,
18.0057560400077));
#156394=CARTESIAN_POINT('Ctrl Pts',(-19.1976024237123,-16.4328243541992,
18.0100722027467));
#156395=CARTESIAN_POINT('Ctrl Pts',(-19.1116786655142,-16.4185210722995,
18.0143883654857));
#156396=CARTESIAN_POINT('Ctrl Pts',(-19.0253143284881,-16.4086290160463,
18.0187045282247));
#156397=CARTESIAN_POINT('Ctrl Pts',(-18.941763300659,-16.3990591924853,
18.0228800924163));
#156398=CARTESIAN_POINT('Ctrl Pts',(-18.8578004300247,-16.3936175999791,
18.027055656608));
#156399=CARTESIAN_POINT('Ctrl Pts',(-18.7738638919263,-16.3923103957471,
18.0312312207996));
#156400=CARTESIAN_POINT('Ctrl Pts',(-18.6856879188252,-16.3909371677368,
18.0356176828123));
#156401=CARTESIAN_POINT('Ctrl Pts',(-18.5975415917826,-16.3941269389876,
18.0400041448249));
#156402=CARTESIAN_POINT('Ctrl Pts',(-18.5099274935592,-16.4018251997447,
18.0443906068376));
#156403=CARTESIAN_POINT('Ctrl Pts',(-18.4223133953358,-16.4095234605017,
18.0487770688502));
#156404=CARTESIAN_POINT('Ctrl Pts',(-18.3352320899718,-16.4217300548923,
18.0531635308629));
#156405=CARTESIAN_POINT('Ctrl Pts',(-18.249172131343,-16.4383289917387,
18.0575499928756));
#156406=CARTESIAN_POINT('Ctrl Pts',(-18.1670719189866,-16.4541641868944,
18.0617346272685));
#156407=CARTESIAN_POINT('Ctrl Pts',(-18.0855955387245,-16.4740553519455,
18.0659192616615));
#156408=CARTESIAN_POINT('Ctrl Pts',(-18.0051743135503,-16.4979394630998,
18.0701038960544));
#156409=CARTESIAN_POINT('Ctrl Pts',(-17.924867558036,-16.5217895781781,
18.0742825741382));
#156410=CARTESIAN_POINT('Ctrl Pts',(-17.8456134116216,-16.5496212203606,
18.0784612522221));
#156411=CARTESIAN_POINT('Ctrl Pts',(-17.7678335788524,-16.5813202564144,
18.0826399303059));
#156412=CARTESIAN_POINT('Ctrl Pts',(-17.6886595984777,-16.6135874749089,
18.0868935081914));
#156413=CARTESIAN_POINT('Ctrl Pts',(-17.6110137791771,-16.6498620057512,
18.0911470860768));
#156414=CARTESIAN_POINT('Ctrl Pts',(-17.5353253711178,-16.6899701297122,
18.0954006639623));
#156415=CARTESIAN_POINT('Ctrl Pts',(-17.4611043305451,-16.7293006794244,
18.0995717779401));
#156416=CARTESIAN_POINT('Ctrl Pts',(-17.3887659072351,-16.7723172800339,
18.103742891918));
#156417=CARTESIAN_POINT('Ctrl Pts',(-17.318693590526,-16.818808080059,18.1079140058958));
#156418=CARTESIAN_POINT('Ctrl Pts',(-17.2486447872595,-16.8652832796471,
18.1120837202161));
#156419=CARTESIAN_POINT('Ctrl Pts',(-17.1808609634159,-16.9152301092319,
18.1162534345363));
#156420=CARTESIAN_POINT('Ctrl Pts',(-17.1156979943011,-16.968392524124,
18.1204231488566));
#156421=CARTESIAN_POINT('Ctrl Pts',(-17.0505373439644,-17.0215530472694,
18.1245927148005));
#156422=CARTESIAN_POINT('Ctrl Pts',(-16.9879977188453,-17.0779286367475,
18.1287622807445));
#156423=CARTESIAN_POINT('Ctrl Pts',(-16.928402088408,-17.1372228286496,
18.1329318466884));
#156424=CARTESIAN_POINT('Ctrl Pts',(-16.8667111491201,-17.1986017311952,
18.1372480094274));
#156425=CARTESIAN_POINT('Ctrl Pts',(-16.8081754519449,-17.263107918902,
18.1415641721665));
#156426=CARTESIAN_POINT('Ctrl Pts',(-16.7531104204836,-17.330372276457,
18.1458803349055));
#156427=CARTESIAN_POINT('Ctrl Pts',(-16.6998391266334,-17.3954455046358,
18.1500558990971));
#156428=CARTESIAN_POINT('Ctrl Pts',(-16.6498160990941,-17.4630995606101,
18.1542314632887));
#156429=CARTESIAN_POINT('Ctrl Pts',(-16.6032836911145,-17.5329693410468,
18.1584070274802));
#156430=CARTESIAN_POINT('Ctrl Pts',(-16.5544010418239,-17.6063680779999,
18.162793489493));
#156431=CARTESIAN_POINT('Ctrl Pts',(-16.509371199651,-17.6822117522655,
18.1671799515058));
#156432=CARTESIAN_POINT('Ctrl Pts',(-16.4684203690346,-17.7600482661808,
18.1715664135186));
#156433=CARTESIAN_POINT('Ctrl Pts',(-16.4274695384181,-17.8378847800961,
18.1759528755314));
#156434=CARTESIAN_POINT('Ctrl Pts',(-16.390597893598,-17.9177135750216,
18.1803393375442));
#156435=CARTESIAN_POINT('Ctrl Pts',(-16.3579723492966,-17.9990610706384,
18.184725799557));
#156436=CARTESIAN_POINT('Ctrl Pts',(-16.3268479546497,-18.0766656473996,
18.1889104339505));
#156437=CARTESIAN_POINT('Ctrl Pts',(-16.2994716572955,-18.1559410996701,
18.193095068344));
#156438=CARTESIAN_POINT('Ctrl Pts',(-16.2760239311543,-18.236490639487,
18.1972797027375));
#156439=CARTESIAN_POINT('Ctrl Pts',(-16.2526095799489,-18.3169255270041,
18.2014583808218));
#156440=CARTESIAN_POINT('Ctrl Pts',(-16.2331128202904,-18.398630461953,
18.2056370589062));
#156441=CARTESIAN_POINT('Ctrl Pts',(-16.217665944864,-18.4811890793931,
18.2098157369906));
#156442=CARTESIAN_POINT('Ctrl Pts',(-16.201942195299,-18.565227500706,18.2140693148759));
#156443=CARTESIAN_POINT('Ctrl Pts',(-16.1904151258529,-18.6501500625611,
18.2183228927612));
#156444=CARTESIAN_POINT('Ctrl Pts',(-16.1831710111198,-18.7355018025745,
18.2225764706466));
#156445=CARTESIAN_POINT('Ctrl Pts',(-16.1760673376856,-18.8191988325684,
18.226747584625));
#156446=CARTESIAN_POINT('Ctrl Pts',(-16.1730820747445,-18.9033080688141,
18.2309186986034));
#156447=CARTESIAN_POINT('Ctrl Pts',(-16.1742446642318,-18.9873923862777,
18.2350898125817));
#156448=CARTESIAN_POINT('Ctrl Pts',(-16.1754068636011,-19.0714484884366,
18.2392595269026));
#156449=CARTESIAN_POINT('Ctrl Pts',(-16.180714144804,-19.1554792288139,
18.2434292412234));
#156450=CARTESIAN_POINT('Ctrl Pts',(-16.1901438433303,-19.2390467804617,
18.2475989555442));
#156451=CARTESIAN_POINT('Ctrl Pts',(-16.1995732063073,-19.3226113584171,
18.2517685214886));
#156452=CARTESIAN_POINT('Ctrl Pts',(-16.2131246425145,-19.4057123233777,
18.2559380874331));
#156453=CARTESIAN_POINT('Ctrl Pts',(-16.2307236899664,-19.4879176388443,
18.2601076533776));
#156454=CARTESIAN_POINT('Ctrl Pts',(-16.2489414982118,-19.5730131917728,
18.264423816116));
#156455=CARTESIAN_POINT('Ctrl Pts',(-16.2714967310845,-19.6571484255567,
18.2687399788544));
#156456=CARTESIAN_POINT('Ctrl Pts',(-16.2982497538328,-19.7398583237465,
18.2730561415928));
#156457=CARTESIAN_POINT('Ctrl Pts',(-16.3241312996848,-19.81987395572,18.2772317057849));
#156458=CARTESIAN_POINT('Ctrl Pts',(-16.3539411382348,-19.8985552629114,
18.281407269977));
#156459=CARTESIAN_POINT('Ctrl Pts',(-16.3875034565753,-19.9755008410822,
18.2855828341691));
#156460=CARTESIAN_POINT('Ctrl Pts',(-16.4227609278168,-20.0563327574592,
18.2899692961806));
#156461=CARTESIAN_POINT('Ctrl Pts',(-16.4621596558346,-20.1352484709666,
18.2943557581922));
#156462=CARTESIAN_POINT('Ctrl Pts',(-16.5054419382129,-20.2118130675793,
18.2987422202037));
#156463=CARTESIAN_POINT('Ctrl Pts',(-16.5487242205912,-20.2883776641921,
18.3031286822153));
#156464=CARTESIAN_POINT('Ctrl Pts',(-16.5958896819153,-20.362590695021,
18.3075151442268));
#156465=CARTESIAN_POINT('Ctrl Pts',(-16.6466304638568,-20.4340554711552,
18.3119016062384));
#156466=CARTESIAN_POINT('Ctrl Pts',(-16.6950307331533,-20.5022238019884,
18.3160857345568));
#156467=CARTESIAN_POINT('Ctrl Pts',(-16.7468638869254,-20.5681455333867,
18.3202698628752));
#156468=CARTESIAN_POINT('Ctrl Pts',(-16.801894064722,-20.6314542729302,
18.3244539911936));
#156469=CARTESIAN_POINT('Ctrl Pts',(-16.8577907043263,-20.69575982199,18.3287039994988));
#156470=CARTESIAN_POINT('Ctrl Pts',(-16.9169857078822,-20.7573689488297,
18.3329540078039));
#156471=CARTESIAN_POINT('Ctrl Pts',(-16.9791857141597,-20.8159277942589,
18.3372040161091));
#156472=CARTESIAN_POINT('Ctrl Pts',(-17.0413857204372,-20.8744866396881,
18.3414540244143));
#156473=CARTESIAN_POINT('Ctrl Pts',(-17.1065904145128,-20.9299948122621,
18.3457040327195));
#156474=CARTESIAN_POINT('Ctrl Pts',(-17.1744641402401,-20.9821349467765,
18.3499540410247));
#156475=CARTESIAN_POINT('Ctrl Pts',(-17.1718942801479,-20.9854857634355,
17.5498940685532));
#156476=CARTESIAN_POINT('Ctrl Pts',(-17.8395944672753,-21.4975646458316,
17.5919369033125));
#156477=CARTESIAN_POINT('Ctrl Pts',(-19.7363287145451,-21.8042998984821,
17.6763716736323));
#156478=CARTESIAN_POINT('Ctrl Pts',(-21.1817725818657,-20.2077259866878,
17.7708370079975));
#156479=CARTESIAN_POINT('Ctrl Pts',(-21.2957663888719,-19.1559927477998,
17.8232595076033));
#156480=CARTESIAN_POINT('Ctrl Pts',(-21.2939116922138,-18.9543565892689,
17.8332900716486));
#156481=CARTESIAN_POINT('',(-21.2939990418858,-18.9497851537328,17.7667099127498));
#156482=CARTESIAN_POINT('Ctrl Pts',(-17.1769969312964,-20.9788274605145,
17.483325298233));
#156483=CARTESIAN_POINT('Ctrl Pts',(-17.5345084118012,-21.2526529396887,
17.505637306168));
#156484=CARTESIAN_POINT('Ctrl Pts',(-18.7708036860181,-21.788223221189,
17.5703412496634));
#156485=CARTESIAN_POINT('Ctrl Pts',(-20.7784813047341,-21.0089843504267,
17.6648027803286));
#156486=CARTESIAN_POINT('Ctrl Pts',(-21.2874612586096,-19.5488856065476,
17.7369523030588));
#156487=CARTESIAN_POINT('Ctrl Pts',(-21.2923872581368,-18.9497870016169,
17.7667098902285));
#156488=CARTESIAN_POINT('Ctrl Pts',(-21.2939990418858,-18.9497851537328,
17.7667099127498));
#156489=CARTESIAN_POINT('Ctrl Pts',(-21.2939112972755,-18.8483667746996,
17.7717442924651));
#156490=CARTESIAN_POINT('Ctrl Pts',(-21.2877929815452,-18.7472123213116,
17.7767786721804));
#156491=CARTESIAN_POINT('Ctrl Pts',(-21.275760552819,-18.64695362298,17.7818130518957));
#156492=CARTESIAN_POINT('Ctrl Pts',(-21.2635573150894,-18.54527168012,17.7869188982619));
#156493=CARTESIAN_POINT('Ctrl Pts',(-21.245270932926,-18.4445110968148,
17.792024744628));
#156494=CARTESIAN_POINT('Ctrl Pts',(-21.2210717431372,-18.345308855769,
17.7971305909941));
#156495=CARTESIAN_POINT('Ctrl Pts',(-21.2092508709201,-18.2968503319384,
17.7996247057963));
#156496=CARTESIAN_POINT('Ctrl Pts',(-21.1960198419216,-18.2487633198847,
17.8021188205986));
#156497=CARTESIAN_POINT('Ctrl Pts',(-21.1814026084241,-18.201120201178,
17.8046129354008));
#156498=CARTESIAN_POINT('Ctrl Pts',(-21.1568777637899,-18.121184412756,
17.8087975697939));
#156499=CARTESIAN_POINT('Ctrl Pts',(-21.1283869296254,-18.0423026572185,
17.8129822041869));
#156500=CARTESIAN_POINT('Ctrl Pts',(-21.0960388974778,-17.9648970434641,
17.8171668385799));
#156501=CARTESIAN_POINT('Ctrl Pts',(-21.0637369087501,-17.88760160702,17.8213455166639));
#156502=CARTESIAN_POINT('Ctrl Pts',(-21.0275888032569,-17.8117785597318,
17.8255241947478));
#156503=CARTESIAN_POINT('Ctrl Pts',(-20.9877531601769,-17.7378349811526,
17.8297028728318));
#156504=CARTESIAN_POINT('Ctrl Pts',(-20.947203491824,-17.6625660170697,
17.8339564507172));
#156505=CARTESIAN_POINT('Ctrl Pts',(-20.9028329287837,-17.5892450243181,
17.8382100286026));
#156506=CARTESIAN_POINT('Ctrl Pts',(-20.8548601014715,-17.5182802121801,
17.8424636064881));
#156507=CARTESIAN_POINT('Ctrl Pts',(-20.8078173210281,-17.448691191402,
17.846634720466));
#156508=CARTESIAN_POINT('Ctrl Pts',(-20.7573109732373,-17.3813682068563,
17.850805834444));
#156509=CARTESIAN_POINT('Ctrl Pts',(-20.7035927080245,-17.3166698912767,
17.8549769484219));
#156510=CARTESIAN_POINT('Ctrl Pts',(-20.6498924684943,-17.2519932858418,
17.8591466627423));
#156511=CARTESIAN_POINT('Ctrl Pts',(-20.5929827456749,-17.1899399538653,
17.8633163770627));
#156512=CARTESIAN_POINT('Ctrl Pts',(-20.533156175962,-17.1308363460419,
17.867486091383));
#156513=CARTESIAN_POINT('Ctrl Pts',(-20.4733317351351,-17.0717348413785,
17.8716556573271));
#156514=CARTESIAN_POINT('Ctrl Pts',(-20.4105909816463,-17.015583174876,
17.8758252232711));
#156515=CARTESIAN_POINT('Ctrl Pts',(-20.345263220069,-16.9626707573524,
17.8799947892151));
#156516=CARTESIAN_POINT('Ctrl Pts',(-20.2776386149851,-16.9078980045031,
17.8843109519541));
#156517=CARTESIAN_POINT('Ctrl Pts',(-20.2072421084912,-16.8565968547186,
17.888627114693));
#156518=CARTESIAN_POINT('Ctrl Pts',(-20.134474432863,-16.8090414462951,
17.8929432774319));
#156519=CARTESIAN_POINT('Ctrl Pts',(-20.0640771566148,-16.7630351502991,
17.8971188416236));
#156520=CARTESIAN_POINT('Ctrl Pts',(-19.9914612509379,-16.7205345053977,
17.9012944058153));
#156521=CARTESIAN_POINT('Ctrl Pts',(-19.9170156443953,-16.6817414276968,
17.905469970007));
#156522=CARTESIAN_POINT('Ctrl Pts',(-19.8388099672436,-16.640989003863,
17.9098564320195));
#156523=CARTESIAN_POINT('Ctrl Pts',(-19.7585854263165,-16.604328771398,
17.9142428940321));
#156524=CARTESIAN_POINT('Ctrl Pts',(-19.6768157184724,-16.5719372863302,
17.9186293560446));
#156525=CARTESIAN_POINT('Ctrl Pts',(-19.5950460106283,-16.5395458012623,
17.9230158180572));
#156526=CARTESIAN_POINT('Ctrl Pts',(-19.5117317099373,-16.5114231770868,
17.9274022800697));
#156527=CARTESIAN_POINT('Ctrl Pts',(-19.427361531773,-16.4876847226344,
17.9317887420823));
#156528=CARTESIAN_POINT('Ctrl Pts',(-19.3468733505732,-16.4650385096604,
17.9359733764753));
#156529=CARTESIAN_POINT('Ctrl Pts',(-19.265124729313,-16.4462975942589,
17.9401580108683));
#156530=CARTESIAN_POINT('Ctrl Pts',(-19.1825294815773,-16.4315989794963,
17.9443426452613));
#156531=CARTESIAN_POINT('Ctrl Pts',(-19.1000517979535,-16.4169212863925,
17.9485213233453));
#156532=CARTESIAN_POINT('Ctrl Pts',(-19.0167303305415,-16.4062745451513,
17.9527000014292));
#156533=CARTESIAN_POINT('Ctrl Pts',(-18.9329932047253,-16.3997457602204,
17.9568786795131));
#156534=CARTESIAN_POINT('Ctrl Pts',(-18.8477551511091,-16.3930999515116,
17.9611322573986));
#156535=CARTESIAN_POINT('Ctrl Pts',(-18.7620868552842,-16.3907213105009,
17.965385835284));
#156536=CARTESIAN_POINT('Ctrl Pts',(-18.6764498971536,-16.3926469595497,
17.9696394131694));
#156537=CARTESIAN_POINT('Ctrl Pts',(-18.5924731785637,-16.394535276134,
17.9738105271474));
#156538=CARTESIAN_POINT('Ctrl Pts',(-18.5085270745237,-16.40056246717,17.9779816411253));
#156539=CARTESIAN_POINT('Ctrl Pts',(-18.4250493517398,-16.4107110559915,
17.9821527551032));
#156540=CARTESIAN_POINT('Ctrl Pts',(-18.341599640712,-16.4208562393561,
17.9863224694236));
#156541=CARTESIAN_POINT('Ctrl Pts',(-18.2586184550888,-16.4351200184238,
17.9904921837439));
#156542=CARTESIAN_POINT('Ctrl Pts',(-18.1765386867733,-16.4534330338661,
17.9946618980643));
#156543=CARTESIAN_POINT('Ctrl Pts',(-18.0944618392082,-16.4717453976528,
17.9988314640083));
#156544=CARTESIAN_POINT('Ctrl Pts',(-18.0132867939826,-16.4941066103199,
18.0030010299523));
#156545=CARTESIAN_POINT('Ctrl Pts',(-17.9334351461144,-16.5203964314216,
18.0071705958963));
#156546=CARTESIAN_POINT('Ctrl Pts',(-17.8507760128139,-16.5476105702015,
18.0114867586353));
#156547=CARTESIAN_POINT('Ctrl Pts',(-17.7695355706378,-16.5790345522992,
18.0158029213742));
#156548=CARTESIAN_POINT('Ctrl Pts',(-17.6901612352904,-16.6144798111482,
18.0201190841132));
#156549=CARTESIAN_POINT('Ctrl Pts',(-17.613372510569,-16.6487704444181,
18.0242946483048));
#156550=CARTESIAN_POINT('Ctrl Pts',(-17.5383305816066,-16.6868241363793,
18.0284702124965));
#156551=CARTESIAN_POINT('Ctrl Pts',(-17.4654157475491,-16.7284231530182,
18.0326457766881));
#156552=CARTESIAN_POINT('Ctrl Pts',(-17.3888181585608,-16.7721232370958,
18.0370322387007));
#156553=CARTESIAN_POINT('Ctrl Pts',(-17.3145686822397,-16.81973589169,18.0414187007133));
#156554=CARTESIAN_POINT('Ctrl Pts',(-17.2430721773899,-16.8709583791363,
18.0458051627259));
#156555=CARTESIAN_POINT('Ctrl Pts',(-17.1715756725401,-16.9221808665826,
18.0501916247385));
#156556=CARTESIAN_POINT('Ctrl Pts',(-17.1028325453263,-16.9770127656117,
18.0545780867511));
#156557=CARTESIAN_POINT('Ctrl Pts',(-17.03720428459,-17.0351055584185,18.0589645487636));
#156558=CARTESIAN_POINT('Ctrl Pts',(-16.9745956774142,-17.0905254157143,
18.0631491831567));
#156559=CARTESIAN_POINT('Ctrl Pts',(-16.9145885551718,-17.1491189671382,
18.0673338175499));
#156560=CARTESIAN_POINT('Ctrl Pts',(-16.8575221052052,-17.2106124181141,
18.071518451943));
#156561=CARTESIAN_POINT('Ctrl Pts',(-16.8005368822667,-17.2720183407739,
18.075697130027));
#156562=CARTESIAN_POINT('Ctrl Pts',(-16.7464843277719,-17.3363156298582,
18.079875808111));
#156563=CARTESIAN_POINT('Ctrl Pts',(-16.6956693348428,-17.4031913935286,
18.084054486195));
#156564=CARTESIAN_POINT('Ctrl Pts',(-16.6439435196865,-17.4712658571988,
18.0883080640804));
#156565=CARTESIAN_POINT('Ctrl Pts',(-16.5955728353228,-17.5420118234209,
18.0925616419658));
#156566=CARTESIAN_POINT('Ctrl Pts',(-16.5508383402301,-17.6150612701733,
18.0968152198512));
#156567=CARTESIAN_POINT('Ctrl Pts',(-16.5069711106161,-17.6866945108574,
18.1009863338293));
#156568=CARTESIAN_POINT('Ctrl Pts',(-16.4666005905003,-17.7605423037905,
18.1051574478073));
#156569=CARTESIAN_POINT('Ctrl Pts',(-16.4299490395872,-17.836227096663,
18.1093285617853));
#156570=CARTESIAN_POINT('Ctrl Pts',(-16.3933097874561,-17.9118864927724,
18.1134982761057));
#156571=CARTESIAN_POINT('Ctrl Pts',(-16.3603872264447,-17.989381250901,
18.1176679904261));
#156572=CARTESIAN_POINT('Ctrl Pts',(-16.331357352511,-18.0683098345761,
18.1218377047466));
#156573=CARTESIAN_POINT('Ctrl Pts',(-16.3023285115847,-18.1472356096334,
18.1260072706907));
#156574=CARTESIAN_POINT('Ctrl Pts',(-16.2771922403253,-18.227594676743,
18.1301768366348));
#156575=CARTESIAN_POINT('Ctrl Pts',(-16.2560756369329,-18.3089674573409,
18.1343464025789));
#156576=CARTESIAN_POINT('Ctrl Pts',(-16.2342165998161,-18.393201204518,
18.1386625653177));
#156577=CARTESIAN_POINT('Ctrl Pts',(-16.2166652853052,-18.478520765314,
18.1429787280566));
#156578=CARTESIAN_POINT('Ctrl Pts',(-16.203505316394,-18.5644478664209,
18.1472948907955));
#156579=CARTESIAN_POINT('Ctrl Pts',(-16.1907740320855,-18.6475759012497,
18.1514704549872));
#156580=CARTESIAN_POINT('Ctrl Pts',(-16.1821523920334,-18.7312720295791,
18.1556460191789));
#156581=CARTESIAN_POINT('Ctrl Pts',(-16.177663165104,-18.8150986247193,
18.1598215833707));
#156582=CARTESIAN_POINT('Ctrl Pts',(-16.1729471979947,-18.9031591018972,
18.1642080453831));
#156583=CARTESIAN_POINT('Ctrl Pts',(-16.172792072363,-18.9913629881318,
18.1685945073955));
#156584=CARTESIAN_POINT('Ctrl Pts',(-16.1771623761344,-19.0792059950832,
18.1729809694079));
#156585=CARTESIAN_POINT('Ctrl Pts',(-16.1815326799057,-19.1670490020346,
18.1773674314203));
#156586=CARTESIAN_POINT('Ctrl Pts',(-16.1904282787085,-19.2545305601574,
18.1817538934327));
#156587=CARTESIAN_POINT('Ctrl Pts',(-16.2037517912765,-19.3411580684653,
18.1861403554451));
#156588=CARTESIAN_POINT('Ctrl Pts',(-16.2164587426292,-19.4237767869345,
18.1903238287685));
#156589=CARTESIAN_POINT('Ctrl Pts',(-16.2332401386084,-19.5059261893906,
18.1945073020919));
#156590=CARTESIAN_POINT('Ctrl Pts',(-16.2540494029908,-19.587173233373,
18.1986907754153));
#156591=CARTESIAN_POINT('Ctrl Pts',(-16.2748315365081,-19.6683143484509,
18.2028687943773));
#156592=CARTESIAN_POINT('Ctrl Pts',(-16.2996310005511,-19.7485549992219,
18.2070468133392));
#156593=CARTESIAN_POINT('Ctrl Pts',(-16.3283498001384,-19.8274696544744,
18.2112248323011));
#156594=CARTESIAN_POINT('Ctrl Pts',(-16.3570397744387,-19.9063051024616,
18.2153986577523));
#156595=CARTESIAN_POINT('Ctrl Pts',(-16.3896411161759,-19.9838167680114,
18.2195724832034));
#156596=CARTESIAN_POINT('Ctrl Pts',(-16.4260056863287,-20.0595929974775,
18.2237463086546));
#156597=CARTESIAN_POINT('Ctrl Pts',(-16.4623446674756,-20.1353159047572,
18.22791719707));
#156598=CARTESIAN_POINT('Ctrl Pts',(-16.5024414177659,-20.2093053885233,
18.2320880854853));
#156599=CARTESIAN_POINT('Ctrl Pts',(-16.5460997340582,-20.2811698259785,
18.2362589739007));
#156600=CARTESIAN_POINT('Ctrl Pts',(-16.5897512956127,-20.3530231446947,
18.2404292170036));
#156601=CARTESIAN_POINT('Ctrl Pts',(-16.6369631004863,-20.4227516709472,
18.2445994601065));
#156602=CARTESIAN_POINT('Ctrl Pts',(-16.6874935461469,-20.4899893804372,
18.2487697032093));
#156603=CARTESIAN_POINT('Ctrl Pts',(-16.7380175638218,-20.5572185366079,
18.2529394158149));
#156604=CARTESIAN_POINT('Ctrl Pts',(-16.7918591019332,-20.6219571415253,
18.2571091284205));
#156605=CARTESIAN_POINT('Ctrl Pts',(-16.8487348978594,-20.68387051902,18.2612788410261));
#156606=CARTESIAN_POINT('Ctrl Pts',(-16.9056490538446,-20.7458256541865,
18.2654513659075));
#156607=CARTESIAN_POINT('Ctrl Pts',(-16.9656012405057,-20.8049514194522,
18.2696238907889));
#156608=CARTESIAN_POINT('Ctrl Pts',(-17.0282702917711,-20.8609489680097,
18.2737964156702));
#156609=CARTESIAN_POINT('Ctrl Pts',(-17.0755086445449,-20.9031585100375,
18.2769415598574));
#156610=CARTESIAN_POINT('Ctrl Pts',(-17.1242898505219,-20.9435913986356,
18.2800867040446));
#156611=CARTESIAN_POINT('Ctrl Pts',(-17.1744641402402,-20.9821349467765,
18.2832318482317));
#156612=CARTESIAN_POINT('Origin',(-18.734,-18.952,-1.76670989022851));
#156613=CARTESIAN_POINT('',(-17.1767158074852,-20.9792339848999,19.149828714141));
#156614=CARTESIAN_POINT('',(-17.1744641402401,-20.9821349467764,19.0833436902736));
#156615=CARTESIAN_POINT('',(-17.1744641402401,-20.9821349467765,-1.76670989022851));
#156616=CARTESIAN_POINT('',(-21.2936055493641,-18.9516176052657,18.6332901348852));
#156617=CARTESIAN_POINT('Ctrl Pts',(-21.2898370902887,-18.9516133246636,
18.6332903748308));
#156618=CARTESIAN_POINT('Ctrl Pts',(-21.2903731169848,-18.5470182197254,
18.6533365919814));
#156619=CARTESIAN_POINT('Ctrl Pts',(-21.0089153450218,-17.2875283998103,
18.7157747446925));
#156620=CARTESIAN_POINT('Ctrl Pts',(-19.0350903615485,-15.9399184014086,
18.8206048329642));
#156621=CARTESIAN_POINT('Ctrl Pts',(-16.3642905510741,-17.0684480147839,
18.9477806396456));
#156622=CARTESIAN_POINT('Ctrl Pts',(-15.9356498827334,-19.5334126702652,
19.0575219333712));
#156623=CARTESIAN_POINT('Ctrl Pts',(-16.7788811058708,-20.6706543117871,
19.1248712915363));
#156624=CARTESIAN_POINT('Ctrl Pts',(-17.1767158074852,-20.9792339848999,
19.149828714141));
#156625=CARTESIAN_POINT('Ctrl Pts',(-17.1744641402401,-20.9821349467765,
18.3499540410247));
#156626=CARTESIAN_POINT('Ctrl Pts',(-17.2410773843612,-21.033306787893,
18.3541251225104));
#156627=CARTESIAN_POINT('Ctrl Pts',(-17.3102609913822,-21.0812343275469,
18.3582962039961));
#156628=CARTESIAN_POINT('Ctrl Pts',(-17.3816628382274,-21.1256568728502,
18.3624672854819));
#156629=CARTESIAN_POINT('Ctrl Pts',(-17.4530410707598,-21.1700647265463,
18.3666369874904));
#156630=CARTESIAN_POINT('Ctrl Pts',(-17.5266356958207,-21.2109696452565,
18.3708066894989));
#156631=CARTESIAN_POINT('Ctrl Pts',(-17.602065883165,-21.2481544275473,
18.3749763915074));
#156632=CARTESIAN_POINT('Ctrl Pts',(-17.6774937511192,-21.2853380664494,
18.3791459653024));
#156633=CARTESIAN_POINT('Ctrl Pts',(-17.754756656113,-21.3188015937751,
18.3833155390974));
#156634=CARTESIAN_POINT('Ctrl Pts',(-17.8334506937448,-21.3483745423041,
18.3874851128924));
#156635=CARTESIAN_POINT('Ctrl Pts',(-17.9145942070361,-21.3788679953565,
18.391784471228));
#156636=CARTESIAN_POINT('Ctrl Pts',(-17.9972589386759,-21.4052244645523,
18.3960838295637));
#156637=CARTESIAN_POINT('Ctrl Pts',(-18.0809835220192,-21.4273119963927,
18.4003831878993));
#156638=CARTESIAN_POINT('Ctrl Pts',(-18.1622979460154,-21.4487636997919,
18.4045587816455));
#156639=CARTESIAN_POINT('Ctrl Pts',(-18.244611554837,-21.4661888816975,
18.4087343753917));
#156640=CARTESIAN_POINT('Ctrl Pts',(-18.3274915789467,-21.4795187246809,
18.412909969138));
#156641=CARTESIAN_POINT('Ctrl Pts',(-18.4140564486528,-21.4934412124391,
18.4172712097683));
#156642=CARTESIAN_POINT('Ctrl Pts',(-18.5012387072319,-21.502895666993,
18.4216324503986));
#156643=CARTESIAN_POINT('Ctrl Pts',(-18.5885418386308,-21.5078642223896,
18.4259936910289));
#156644=CARTESIAN_POINT('Ctrl Pts',(-18.6758449700296,-21.5128327777861,
18.4303549316592));
#156645=CARTESIAN_POINT('Ctrl Pts',(-18.7632684101765,-21.5133155051365,
18.4347161722895));
#156646=CARTESIAN_POINT('Ctrl Pts',(-18.8503205710794,-21.5093559636358,
18.4390774129198));
#156647=CARTESIAN_POINT('Ctrl Pts',(-18.9338475986689,-21.5055567617696,
18.4432620473123));
#156648=CARTESIAN_POINT('Ctrl Pts',(-19.0173437395027,-21.4976540121366,
18.4474466817047));
#156649=CARTESIAN_POINT('Ctrl Pts',(-19.1003730904689,-21.4856477179317,
18.4516313160972));
#156650=CARTESIAN_POINT('Ctrl Pts',(-19.1832842594309,-21.4736585132005,
18.4558099941805));
#156651=CARTESIAN_POINT('Ctrl Pts',(-19.2657295068645,-21.4575774310127,
18.4599886722639));
#156652=CARTESIAN_POINT('Ctrl Pts',(-19.3472750579131,-21.437456437627,
18.4641673503472));
#156653=CARTESIAN_POINT('Ctrl Pts',(-19.4302822543734,-21.4169747898919,
18.4684209282328));
#156654=CARTESIAN_POINT('Ctrl Pts',(-19.5123567014418,-21.3923069974992,
18.4726745061184));
#156655=CARTESIAN_POINT('Ctrl Pts',(-19.5930485432779,-21.3635628957778,
18.476928084004));
#156656=CARTESIAN_POINT('Ctrl Pts',(-19.6721760162886,-21.3353760545629,
18.4810991979813));
#156657=CARTESIAN_POINT('Ctrl Pts',(-19.7499735613546,-21.3032697094725,
18.4852703119587));
#156658=CARTESIAN_POINT('Ctrl Pts',(-19.8260310897304,-21.2673980433313,
18.489441425936));
#156659=CARTESIAN_POINT('Ctrl Pts',(-19.9020630962678,-21.2315384142742,
18.4936111402558));
#156660=CARTESIAN_POINT('Ctrl Pts',(-19.9763558299771,-21.1919161695522,
18.4977808545756));
#156661=CARTESIAN_POINT('Ctrl Pts',(-20.0485201368017,-21.1487332131925,
18.5019505688953));
#156662=CARTESIAN_POINT('Ctrl Pts',(-20.1206818757106,-21.1055517934676,
18.5061201348388));
#156663=CARTESIAN_POINT('Ctrl Pts',(-20.1907149440062,-21.058810150979,
18.5102897007822));
#156664=CARTESIAN_POINT('Ctrl Pts',(-20.2582569041575,-21.0087549416807,
18.5144592667256));
#156665=CARTESIAN_POINT('Ctrl Pts',(-20.3281735563277,-20.9569398529571,
18.5187754294653));
#156666=CARTESIAN_POINT('Ctrl Pts',(-20.3954202425923,-20.9015741660665,
18.5230915922049));
#156667=CARTESIAN_POINT('Ctrl Pts',(-20.4596314884386,-20.8429775160242,
18.5274077549445));
#156668=CARTESIAN_POINT('Ctrl Pts',(-20.5217510596858,-20.7862896457116,
18.5315833191356));
#156669=CARTESIAN_POINT('Ctrl Pts',(-20.5810296141589,-20.7265784444846,
18.5357588833267));
#156670=CARTESIAN_POINT('Ctrl Pts',(-20.6371745600421,-20.6641701416649,
18.5399344475178));
#156671=CARTESIAN_POINT('Ctrl Pts',(-20.6961552536971,-20.5986097438011,
18.5443209095317));
#156672=CARTESIAN_POINT('Ctrl Pts',(-20.7516770948084,-20.5300730764183,
18.5487073715456));
#156673=CARTESIAN_POINT('Ctrl Pts',(-20.8034508935152,-20.4589747839062,
18.5530938335595));
#156674=CARTESIAN_POINT('Ctrl Pts',(-20.8552246922221,-20.387876491394,
18.5574802955735));
#156675=CARTESIAN_POINT('Ctrl Pts',(-20.9032501953501,-20.3142171013321,
18.5618667575874));
#156676=CARTESIAN_POINT('Ctrl Pts',(-20.9472937739973,-20.238441086869,
18.5662532196013));
#156677=CARTESIAN_POINT('Ctrl Pts',(-20.9909726387703,-20.1632925546555,
18.5706033584189));
#156678=CARTESIAN_POINT('Ctrl Pts',(-21.0308877830082,-20.0858014915382,
18.5749534972364));
#156679=CARTESIAN_POINT('Ctrl Pts',(-21.066791372662,-20.0063644586356,
18.579303636054));
#156680=CARTESIAN_POINT('Ctrl Pts',(-21.1039225287105,-19.9242114234328,
18.5838025088638));
#156681=CARTESIAN_POINT('Ctrl Pts',(-21.1367625751618,-19.839977276334,
18.5883013816736));
#156682=CARTESIAN_POINT('Ctrl Pts',(-21.1650869626509,-19.7541322709059,
18.5928002544834));
#156683=CARTESIAN_POINT('Ctrl Pts',(-21.1923645588308,-19.6714598603191,
18.5971328613515));
#156684=CARTESIAN_POINT('Ctrl Pts',(-21.2154541944231,-19.5872939815202,
18.6014654682196));
#156685=CARTESIAN_POINT('Ctrl Pts',(-21.2342029378176,-19.5020775124729,
18.6057980750877));
#156686=CARTESIAN_POINT('Ctrl Pts',(-21.252927481766,-19.4169710343355,
18.6101250897577));
#156687=CARTESIAN_POINT('Ctrl Pts',(-21.267322189726,-19.330817060707,18.6144521044277));
#156688=CARTESIAN_POINT('Ctrl Pts',(-21.2772839154191,-19.2440734934402,
18.6187791190978));
#156689=CARTESIAN_POINT('Ctrl Pts',(-21.2872318317731,-19.1574501735453,
18.6231001354886));
#156690=CARTESIAN_POINT('Ctrl Pts',(-21.2927589555484,-19.0702392928319,
18.6274211518793));
#156691=CARTESIAN_POINT('Ctrl Pts',(-21.2938134141943,-18.9829076772209,
18.6317421682701));
#156692=CARTESIAN_POINT('Ctrl Pts',(-21.2939393290371,-18.9724792486627,
18.6322581487706));
#156693=CARTESIAN_POINT('Ctrl Pts',(-21.2940015277989,-18.9620491070299,
18.632774129271));
#156694=CARTESIAN_POINT('Ctrl Pts',(-21.2939999715072,-18.9516180532908,
18.6332901097715));
#156695=CARTESIAN_POINT('',(-21.2939999971965,-18.9518801919504,18.5667098901964));
#156696=CARTESIAN_POINT('Ctrl Pts',(-17.1744641402402,-20.9821349467765,
18.2832318482317));
#156697=CARTESIAN_POINT('Ctrl Pts',(-17.2411082793406,-21.0333305212062,
18.2874093946978));
#156698=CARTESIAN_POINT('Ctrl Pts',(-17.3102108974908,-21.0811910583105,
18.2915869411639));
#156699=CARTESIAN_POINT('Ctrl Pts',(-17.3813969214214,-21.1254914105696,
18.29576448763));
#156700=CARTESIAN_POINT('Ctrl Pts',(-17.4526989816651,-21.1698639743284,
18.2999488436784));
#156701=CARTESIAN_POINT('Ctrl Pts',(-17.5260908238986,-21.2106645484754,
18.3041331997268));
#156702=CARTESIAN_POINT('Ctrl Pts',(-17.601173651747,-21.2477143691461,
18.3083175557752));
#156703=CARTESIAN_POINT('Ctrl Pts',(-17.6310714819674,-21.2624675328168,
18.3099837578923));
#156704=CARTESIAN_POINT('Ctrl Pts',(-17.6612372295859,-21.2766265133864,
18.3116499600094));
#156705=CARTESIAN_POINT('Ctrl Pts',(-17.6916449845513,-21.2901822045702,
18.3133161621265));
#156706=CARTESIAN_POINT('Ctrl Pts',(-17.7680134730656,-21.3242270608135,
18.3175007965194));
#156707=CARTESIAN_POINT('Ctrl Pts',(-17.8461937671324,-21.3545898770089,
18.3216854309123));
#156708=CARTESIAN_POINT('Ctrl Pts',(-17.925796207947,-21.3810752624221,
18.3258700653053));
#156709=CARTESIAN_POINT('Ctrl Pts',(-18.0052853445399,-21.4075229491675,
18.3300487433891));
#156710=CARTESIAN_POINT('Ctrl Pts',(-18.0861921743113,-21.4301040236941,
18.3342274214729));
#156711=CARTESIAN_POINT('Ctrl Pts',(-18.1681056484756,-21.4486704994678,
18.3384060995568));
#156712=CARTESIAN_POINT('Ctrl Pts',(-18.251487362797,-21.4675697659769,
18.3426596774422));
#156713=CARTESIAN_POINT('Ctrl Pts',(-18.3359117243118,-21.4823088984315,
18.3469132553277));
#156714=CARTESIAN_POINT('Ctrl Pts',(-18.4209273694976,-21.4927844316333,
18.3511668332132));
#156715=CARTESIAN_POINT('Ctrl Pts',(-18.5042948205042,-21.5030568761823,
18.355337947191));
#156716=CARTESIAN_POINT('Ctrl Pts',(-18.5882303557904,-21.5092295037566,
18.3595090611688));
#156717=CARTESIAN_POINT('Ctrl Pts',(-18.6722982811996,-21.5112563173502,
18.3636801751467));
#156718=CARTESIAN_POINT('Ctrl Pts',(-18.7563379968046,-21.513282450827,
18.3678498894669));
#156719=CARTESIAN_POINT('Ctrl Pts',(-18.8405095547876,-21.5111655221263,
18.3720196037872));
#156720=CARTESIAN_POINT('Ctrl Pts',(-18.9243745836511,-21.5049115765924,
18.3761893181074));
#156721=CARTESIAN_POINT('Ctrl Pts',(-19.0082366282369,-21.4986578536008,
18.3803588840514));
#156722=CARTESIAN_POINT('Ctrl Pts',(-19.0917917066946,-21.4882674415332,
18.3845284499953));
#156723=CARTESIAN_POINT('Ctrl Pts',(-19.1746052695948,-21.4737983655331,
18.3886980159392));
#156724=CARTESIAN_POINT('Ctrl Pts',(-19.2603304552102,-21.4588205746695,
18.3930141786783));
#156725=CARTESIAN_POINT('Ctrl Pts',(-19.3452604921636,-21.4394720625983,
18.3973303414173));
#156726=CARTESIAN_POINT('Ctrl Pts',(-19.4289254033754,-21.4158747297181,
18.4016465041564));
#156727=CARTESIAN_POINT('Ctrl Pts',(-19.5098649388997,-21.3930460774759,
18.405822068348));
#156728=CARTESIAN_POINT('Ctrl Pts',(-19.5896200744145,-21.3662413589924,
18.4099976325395));
#156729=CARTESIAN_POINT('Ctrl Pts',(-19.6677830273837,-21.3356210390434,
18.4141731967311));
#156730=CARTESIAN_POINT('Ctrl Pts',(-19.7498938052997,-21.3034541595238,
18.4185596587439));
#156731=CARTESIAN_POINT('Ctrl Pts',(-19.8302467994652,-21.2670763374215,
18.4229461207567));
#156732=CARTESIAN_POINT('Ctrl Pts',(-19.9083976363218,-21.226728597394,
18.4273325827695));
#156733=CARTESIAN_POINT('Ctrl Pts',(-19.9865484731783,-21.1863808573664,
18.4317190447823));
#156734=CARTESIAN_POINT('Ctrl Pts',(-20.0624966899234,-21.1420635575359,
18.4361055067951));
#156735=CARTESIAN_POINT('Ctrl Pts',(-20.1358342086536,-21.0940692919344,
18.4404919688079));
#156736=CARTESIAN_POINT('Ctrl Pts',(-20.2057039471169,-21.0483444454524,
18.4446710160258));
#156737=CARTESIAN_POINT('Ctrl Pts',(-20.2734659150701,-20.9991112651902,
18.4488500632436));
#156738=CARTESIAN_POINT('Ctrl Pts',(-20.3387454860835,-20.9465906660001,
18.4530291104615));
#156739=CARTESIAN_POINT('Ctrl Pts',(-20.4039320790896,-20.8941448721524,
18.4572022054423));
#156740=CARTESIAN_POINT('Ctrl Pts',(-20.46664294125,-20.8384212459577,18.461375300423));
#156741=CARTESIAN_POINT('Ctrl Pts',(-20.5265316718116,-20.7796843834624,
18.4655483954038));
#156742=CARTESIAN_POINT('Ctrl Pts',(-20.5870226816093,-20.7203568256503,
18.4697634576868));
#156743=CARTESIAN_POINT('Ctrl Pts',(-20.6446340707897,-20.6579553356914,
18.4739785199699));
#156744=CARTESIAN_POINT('Ctrl Pts',(-20.6990425114804,-20.5927949073771,
18.4781935822529));
#156745=CARTESIAN_POINT('Ctrl Pts',(-20.7528122887531,-20.528399352699,
18.4823591668069));
#156746=CARTESIAN_POINT('Ctrl Pts',(-20.803453612438,-20.4613096522777,
18.4865247513609));
#156747=CARTESIAN_POINT('Ctrl Pts',(-20.8506921231955,-20.3918661241943,
18.4906903359149));
#156748=CARTESIAN_POINT('Ctrl Pts',(-20.8979149500345,-20.3224456524396,
18.4948545374302));
#156749=CARTESIAN_POINT('Ctrl Pts',(-20.9417369482816,-20.2506732862343,
18.4990187389455));
#156750=CARTESIAN_POINT('Ctrl Pts',(-20.9819260328718,-20.1769198140031,
18.5031829404608));
#156751=CARTESIAN_POINT('Ctrl Pts',(-21.0221139173366,-20.1031685441961,
18.5073470176248));
#156752=CARTESIAN_POINT('Ctrl Pts',(-21.0586688839111,-20.0274366916314,
18.5115110947889));
#156753=CARTESIAN_POINT('Ctrl Pts',(-21.0914046022627,-19.9501200034218,
18.5156751719529));
#156754=CARTESIAN_POINT('Ctrl Pts',(-21.1248385440614,-19.8711542197507,
18.5199280651399));
#156755=CARTESIAN_POINT('Ctrl Pts',(-21.1542882228969,-19.7905356687051,
18.5241809583268));
#156756=CARTESIAN_POINT('Ctrl Pts',(-21.1796074785074,-19.7087060598863,
18.5284338515138));
#156757=CARTESIAN_POINT('Ctrl Pts',(-21.2044336791703,-19.6284699613236,
18.5326039259141));
#156758=CARTESIAN_POINT('Ctrl Pts',(-21.2252888283687,-19.5470700198229,
18.5367740003145));
#156759=CARTESIAN_POINT('Ctrl Pts',(-21.2420864983913,-19.4649348073461,
18.5409440747148));
#156760=CARTESIAN_POINT('Ctrl Pts',(-21.2593845777048,-19.3803527541243,
18.5452383772951));
#156761=CARTESIAN_POINT('Ctrl Pts',(-21.2723795196075,-19.294991452669,
18.5495326798753));
#156762=CARTESIAN_POINT('Ctrl Pts',(-21.2810343673868,-19.2093245642189,
18.5538269824556));
#156763=CARTESIAN_POINT('Ctrl Pts',(-21.2896892151661,-19.1236576757689,
18.5581212850359));
#156764=CARTESIAN_POINT('Ctrl Pts',(-21.2940040128973,-19.0376857298059,
18.5624155876161));
#156765=CARTESIAN_POINT('Ctrl Pts',(-21.2939999971965,-18.9518801919504,
18.5667098901964));
#156766=CARTESIAN_POINT('Ctrl Pts',(-21.2939999971965,-18.9518801913084,
18.5667098902285));
#156767=CARTESIAN_POINT('Ctrl Pts',(-21.2939996986147,-18.945500276023,
18.5670291853155));
#156768=CARTESIAN_POINT('Ctrl Pts',(-21.2939755504833,-18.939120426077,
18.5673484804024));
#156769=CARTESIAN_POINT('Ctrl Pts',(-21.2939275539577,-18.9327407557766,
18.5676677754894));
#156770=CARTESIAN_POINT('Ctrl Pts',(-21.2932985185608,-18.84912973624,18.5718524098819));
#156771=CARTESIAN_POINT('Ctrl Pts',(-21.2885677156651,-18.7653939703417,
18.5760370442745));
#156772=CARTESIAN_POINT('Ctrl Pts',(-21.2797186185528,-18.6819690477864,
18.580221678667));
#156773=CARTESIAN_POINT('Ctrl Pts',(-21.2708821170351,-18.5986628702825,
18.5844003567505));
#156774=CARTESIAN_POINT('Ctrl Pts',(-21.2579390129528,-18.5156671108363,
18.5885790348339));
#156775=CARTESIAN_POINT('Ctrl Pts',(-21.2409247859828,-18.4334172029223,
18.5927577129174));
#156776=CARTESIAN_POINT('Ctrl Pts',(-21.2236055912197,-18.3496930245084,
18.5970112908029));
#156777=CARTESIAN_POINT('Ctrl Pts',(-21.2020678918843,-18.2667421815314,
18.6012648686885));
#156778=CARTESIAN_POINT('Ctrl Pts',(-21.1764043852929,-18.1850183713399,
18.605518446574));
#156779=CARTESIAN_POINT('Ctrl Pts',(-21.1512384158586,-18.1048789366916,
18.6096895605515));
#156780=CARTESIAN_POINT('Ctrl Pts',(-21.1221053294157,-18.02591984166,18.613860674529));
#156781=CARTESIAN_POINT('Ctrl Pts',(-21.0891436468891,-17.9485567268061,
18.6180317885064));
#156782=CARTESIAN_POINT('Ctrl Pts',(-21.0561930249733,-17.8712195718925,
18.6222015028263));
#156783=CARTESIAN_POINT('Ctrl Pts',(-21.0194165386218,-17.7954777564205,
18.6263712171462));
#156784=CARTESIAN_POINT('Ctrl Pts',(-20.9790011895035,-17.721727810959,
18.6305409314661));
#156785=CARTESIAN_POINT('Ctrl Pts',(-20.9385872785368,-17.6479804898368,
18.6347104974097));
#156786=CARTESIAN_POINT('Ctrl Pts',(-20.8945349840831,-17.5762253008168,
18.6388800633532));
#156787=CARTESIAN_POINT('Ctrl Pts',(-20.8470770406693,-17.5068337741989,
18.6430496292968));
#156788=CARTESIAN_POINT('Ctrl Pts',(-20.7979505344986,-17.4350025270909,
18.6473657920363));
#156789=CARTESIAN_POINT('Ctrl Pts',(-20.7451747360216,-17.3657046830186,
18.6516819547758));
#156790=CARTESIAN_POINT('Ctrl Pts',(-20.6890551911698,-17.2993175745231,
18.6559981175153));
#156791=CARTESIAN_POINT('Ctrl Pts',(-20.6347637346021,-17.23509301912,18.6601736817065));
#156792=CARTESIAN_POINT('Ctrl Pts',(-20.5773433873059,-17.173592789127,
18.6643492458977));
#156793=CARTESIAN_POINT('Ctrl Pts',(-20.5171090485652,-17.1151216368728,
18.668524810089));
#156794=CARTESIAN_POINT('Ctrl Pts',(-20.4538324165453,-17.0536972456979,
18.6729112721026));
#156795=CARTESIAN_POINT('Ctrl Pts',(-20.3874504923529,-16.9956163559344,
18.6772977341163));
#156796=CARTESIAN_POINT('Ctrl Pts',(-20.3183666557521,-16.9411836731962,
18.6816841961299));
#156797=CARTESIAN_POINT('Ctrl Pts',(-20.2492828191514,-16.886750990458,
18.6860706581436));
#156798=CARTESIAN_POINT('Ctrl Pts',(-20.1774975877418,-16.835966787744,
18.6904571201572));
#156799=CARTESIAN_POINT('Ctrl Pts',(-20.1034462555221,-16.7890813808105,
18.6948435821709));
#156800=CARTESIAN_POINT('Ctrl Pts',(-20.0328021348959,-16.7443532409684,
18.6990282165633));
#156801=CARTESIAN_POINT('Ctrl Pts',(-19.9598329133702,-16.703006515634,
18.7032128509558));
#156802=CARTESIAN_POINT('Ctrl Pts',(-19.8848959073542,-16.665290877607,
18.7073974853483));
#156803=CARTESIAN_POINT('Ctrl Pts',(-19.810065564891,-16.6276289231225,
18.7115761634316));
#156804=CARTESIAN_POINT('Ctrl Pts',(-19.7332734088094,-16.5935879949175,
18.715754841515));
#156805=CARTESIAN_POINT('Ctrl Pts',(-19.6549047742285,-16.5633739520798,
18.7199335195983));
#156806=CARTESIAN_POINT('Ctrl Pts',(-19.5751314381812,-16.5326183442331,
18.7241870974839));
#156807=CARTESIAN_POINT('Ctrl Pts',(-19.4937249583384,-16.5058284229432,
18.7284406753695));
#156808=CARTESIAN_POINT('Ctrl Pts',(-19.4111169976703,-16.4831718222068,
18.7326942532551));
#156809=CARTESIAN_POINT('Ctrl Pts',(-19.3301105535305,-16.4609544638903,
18.7368653672324));
#156810=CARTESIAN_POINT('Ctrl Pts',(-19.247949263021,-16.4427117186153,
18.7410364812098));
#156811=CARTESIAN_POINT('Ctrl Pts',(-19.1650575928263,-16.4285520905581,
18.7452075951871));
#156812=CARTESIAN_POINT('Ctrl Pts',(-19.0821937377322,-16.4143972139008,
18.7493773095069));
#156813=CARTESIAN_POINT('Ctrl Pts',(-18.9986004427846,-16.4043228107593,
18.7535470238266));
#156814=CARTESIAN_POINT('Ctrl Pts',(-18.9147123478962,-16.3983862767995,
18.7577167381464));
#156815=CARTESIAN_POINT('Ctrl Pts',(-18.8308272381063,-16.3924499540871,
18.7618863040898));
#156816=CARTESIAN_POINT('Ctrl Pts',(-18.7466478081782,-16.3906512394234,
18.7660558700333));
#156817=CARTESIAN_POINT('Ctrl Pts',(-18.6626124310835,-16.3929955422071,
18.7702254359767));
#156818=CARTESIAN_POINT('Ctrl Pts',(-18.5756224737719,-16.3954222677853,
18.7745415987163));
#156819=CARTESIAN_POINT('Ctrl Pts',(-18.4887874147824,-16.4022887536938,
18.778857761456));
#156820=CARTESIAN_POINT('Ctrl Pts',(-18.4025899172854,-16.4135423271059,
18.7831739241956));
#156821=CARTESIAN_POINT('Ctrl Pts',(-18.319200294229,-16.4244293165443,
18.7873494883867));
#156822=CARTESIAN_POINT('Ctrl Pts',(-18.2364077885012,-16.439421833601,
18.7915250525777));
#156823=CARTESIAN_POINT('Ctrl Pts',(-18.1546390975922,-16.4584200544676,
18.7957006167688));
#156824=CARTESIAN_POINT('Ctrl Pts',(-18.0687404644525,-16.4783778303154,
18.8000870787827));
#156825=CARTESIAN_POINT('Ctrl Pts',(-17.9839723511228,-16.5027564393572,
18.8044735407966));
#156826=CARTESIAN_POINT('Ctrl Pts',(-17.9008093086194,-16.5313816344172,
18.8088600028106));
#156827=CARTESIAN_POINT('Ctrl Pts',(-17.8176462661159,-16.5600068294773,
18.8132464648245));
#156828=CARTESIAN_POINT('Ctrl Pts',(-17.7360888041544,-16.5928783231054,
18.8176329268384));
#156829=CARTESIAN_POINT('Ctrl Pts',(-17.6565830150583,-16.6297655931067,
18.8220193888523));
#156830=CARTESIAN_POINT('Ctrl Pts',(-17.5807354051422,-16.6649556251501,
18.8262040232484));
#156831=CARTESIAN_POINT('Ctrl Pts',(-17.5064724966934,-16.70393099464,18.8303886576446));
#156832=CARTESIAN_POINT('Ctrl Pts',(-17.4341976336204,-16.7465263981734,
18.8345732920407));
#156833=CARTESIAN_POINT('Ctrl Pts',(-17.3620256448689,-16.7890611724222,
18.8387519701277));
#156834=CARTESIAN_POINT('Ctrl Pts',(-17.2918364736807,-16.8352055143126,
18.8429306482147));
#156835=CARTESIAN_POINT('Ctrl Pts',(-17.2240117895626,-16.8847468456089,
18.8471093263018));
#156836=CARTESIAN_POINT('Ctrl Pts',(-17.1549713967899,-16.9351761696176,
18.8513629041864));
#156837=CARTESIAN_POINT('Ctrl Pts',(-17.0883815290666,-16.9891252600227,
18.8556164820711));
#156838=CARTESIAN_POINT('Ctrl Pts',(-17.0246167910329,-17.0463218936816,
18.8598700599558));
#156839=CARTESIAN_POINT('Ctrl Pts',(-16.9620882568152,-17.1024096590385,
18.8640411739368));
#156840=CARTESIAN_POINT('Ctrl Pts',(-16.9022766467381,-17.1616198500931,
18.8682122879178));
#156841=CARTESIAN_POINT('Ctrl Pts',(-16.8455029514086,-17.223654288789,
18.8723834018988));
#156842=CARTESIAN_POINT('Ctrl Pts',(-16.7887483070409,-17.2856679112298,
18.8765531162223));
#156843=CARTESIAN_POINT('Ctrl Pts',(-16.7350298631989,-17.3505035600764,
18.8807228305457));
#156844=CARTESIAN_POINT('Ctrl Pts',(-16.6846311428961,-17.4178268391304,
18.8848925448692));
#156845=CARTESIAN_POINT('Ctrl Pts',(-16.6342342159962,-17.4851477225331,
18.8890621108163));
#156846=CARTESIAN_POINT('Ctrl Pts',(-16.5871570527719,-17.5549556913587,
18.8932316767634));
#156847=CARTESIAN_POINT('Ctrl Pts',(-16.5436414846469,-17.6268850713165,
18.8974012427105));
#156848=CARTESIAN_POINT('Ctrl Pts',(-16.4985959629,-17.7013433994214,18.9017174054458));
#156849=CARTESIAN_POINT('Ctrl Pts',(-16.4573674204997,-17.7780746406049,
18.906033568181));
#156850=CARTESIAN_POINT('Ctrl Pts',(-16.4201728243532,-17.8566444407234,
18.9103497309163));
#156851=CARTESIAN_POINT('Ctrl Pts',(-16.3841898382076,-17.9326548379861,
18.914525295111));
#156852=CARTESIAN_POINT('Ctrl Pts',(-16.3519821593661,-18.0103853983063,
18.9187008593057));
#156853=CARTESIAN_POINT('Ctrl Pts',(-16.3236968150621,-18.0894233038864,
18.9228764235003));
#156854=CARTESIAN_POINT('Ctrl Pts',(-16.293982845328,-18.1724532259908,
18.9272628855059));
#156855=CARTESIAN_POINT('Ctrl Pts',(-16.2685980256123,-18.2569254729983,
18.9316493475114));
#156856=CARTESIAN_POINT('Ctrl Pts',(-16.2476527070797,-18.3423467059155,
18.936035809517));
#156857=CARTESIAN_POINT('Ctrl Pts',(-16.2267073885472,-18.4277679388328,
18.9404222715226));
#156858=CARTESIAN_POINT('Ctrl Pts',(-16.210201605397,-18.5141375734783,
18.9448087335281));
#156859=CARTESIAN_POINT('Ctrl Pts',(-16.1981829862585,-18.6009557395151,
18.9491951955337));
#156860=CARTESIAN_POINT('Ctrl Pts',(-16.1867173615959,-18.6837792730849,
18.9533798299225));
#156861=CARTESIAN_POINT('Ctrl Pts',(-16.1792923755172,-18.7673192548711,
18.9575644643113));
#156862=CARTESIAN_POINT('Ctrl Pts',(-16.1759873564286,-18.8511470608817,
18.9617490987001));
#156863=CARTESIAN_POINT('Ctrl Pts',(-16.1726870416255,-18.9348555483864,
18.9659277767798));
#156864=CARTESIAN_POINT('Ctrl Pts',(-16.173495063509,-19.0188505906136,
18.9701064548595));
#156865=CARTESIAN_POINT('Ctrl Pts',(-16.1784392678898,-19.1026961993429,
18.9742851329392));
#156866=CARTESIAN_POINT('Ctrl Pts',(-16.1834720935871,-19.1880446804576,
18.9785387108257));
#156867=CARTESIAN_POINT('Ctrl Pts',(-16.1927909085455,-19.2732378406053,
18.9827922887122));
#156868=CARTESIAN_POINT('Ctrl Pts',(-16.2063695825694,-19.3578133473402,
18.9870458665987));
#156869=CARTESIAN_POINT('Ctrl Pts',(-16.219685007484,-19.4407491927378,
18.9912169805725));
#156870=CARTESIAN_POINT('Ctrl Pts',(-16.2370965177702,-19.5230906447079,
18.9953880945462));
#156871=CARTESIAN_POINT('Ctrl Pts',(-16.2585271389983,-19.6044064028225,
18.99955920852));
#156872=CARTESIAN_POINT('Ctrl Pts',(-16.2799505689745,-19.6856948746497,
19.0037289228362));
#156873=CARTESIAN_POINT('Ctrl Pts',(-16.3053903143092,-19.7659578916982,
19.0078986371525));
#156874=CARTESIAN_POINT('Ctrl Pts',(-16.3347186663492,-19.8447760536633,
19.0120683514687));
#156875=CARTESIAN_POINT('Ctrl Pts',(-16.3640459747607,-19.9235914109407,
19.0162379174086));
#156876=CARTESIAN_POINT('Ctrl Pts',(-16.3972614535251,-20.0009615845047,
19.0204074833485));
#156877=CARTESIAN_POINT('Ctrl Pts',(-16.4341885271963,-20.0764852998419,
19.0245770492885));
#156878=CARTESIAN_POINT('Ctrl Pts',(-16.472413911305,-20.1546643360088,
19.0288932120324));
#156879=CARTESIAN_POINT('Ctrl Pts',(-16.5146165141598,-20.2308641813283,
19.0332093747763));
#156880=CARTESIAN_POINT('Ctrl Pts',(-16.5605485527334,-20.3046672933041,
19.0375255375201));
#156881=CARTESIAN_POINT('Ctrl Pts',(-16.6049843598882,-20.3760662765199,
19.0417011017078));
#156882=CARTESIAN_POINT('Ctrl Pts',(-16.6529100541809,-20.4452219153924,
19.0458766658955));
#156883=CARTESIAN_POINT('Ctrl Pts',(-16.7040581042264,-20.5117871328431,
19.0500522300832));
#156884=CARTESIAN_POINT('Ctrl Pts',(-16.7577895208536,-20.5817144014006,
19.0544386921052));
#156885=CARTESIAN_POINT('Ctrl Pts',(-16.815076991294,-20.6487822429872,
19.0588251541272));
#156886=CARTESIAN_POINT('Ctrl Pts',(-16.8755654265139,-20.7126308346929,
19.0632116161492));
#156887=CARTESIAN_POINT('Ctrl Pts',(-16.9360538617338,-20.7764794263986,
19.0675980781712));
#156888=CARTESIAN_POINT('Ctrl Pts',(-16.9997427890403,-20.8371084232607,
19.0719845401931));
#156889=CARTESIAN_POINT('Ctrl Pts',(-17.066237677054,-20.8942072068041,
19.0763710022151));
#156890=CARTESIAN_POINT('Ctrl Pts',(-17.1014709401622,-20.9244618101855,
19.078695231568));
#156891=CARTESIAN_POINT('Ctrl Pts',(-17.1375640758584,-20.9537885682649,
19.0810194609208));
#156892=CARTESIAN_POINT('Ctrl Pts',(-17.1744641402401,-20.9821349467764,
19.0833436902736));
#156893=CARTESIAN_POINT('Origin',(-18.734,-18.952,-1.76670989022851));
#156894=CARTESIAN_POINT('',(-17.1744641402401,-20.9821349467765,19.9498236254873));
#156895=CARTESIAN_POINT('',(-17.1744641402401,-20.9821349467765,19.8833624839903));
#156896=CARTESIAN_POINT('',(-17.1744641402401,-20.9821349467765,-1.76670989022851));
#156897=CARTESIAN_POINT('',(-21.2939990581247,-18.9498040034555,19.4332901097715));
#156898=CARTESIAN_POINT('Ctrl Pts',(-21.2939990581247,-18.9498040034555,
19.4332901097715));
#156899=CARTESIAN_POINT('Ctrl Pts',(-21.2938905873826,-18.8233534412897,
19.4395926510315));
#156900=CARTESIAN_POINT('Ctrl Pts',(-21.2844099378408,-18.6972910724131,
19.4458951922915));
#156901=CARTESIAN_POINT('Ctrl Pts',(-21.2657470116111,-18.5727150554023,
19.4521977335515));
#156902=CARTESIAN_POINT('Ctrl Pts',(-21.2615163488077,-18.544475158032,
19.4536264444915));
#156903=CARTESIAN_POINT('Ctrl Pts',(-21.25681399964,-18.5163115073431,19.4550551554314));
#156904=CARTESIAN_POINT('Ctrl Pts',(-21.2516424693647,-18.4882367021301,
19.4564838663713));
#156905=CARTESIAN_POINT('Ctrl Pts',(-21.2364952751732,-18.4060067810402,
19.4606685004929));
#156906=CARTESIAN_POINT('Ctrl Pts',(-21.2172870302558,-18.3243667083798,
19.4648531346144));
#156907=CARTESIAN_POINT('Ctrl Pts',(-21.1940771445919,-18.2437483196936,
19.469037768736));
#156908=CARTESIAN_POINT('Ctrl Pts',(-21.1709002953281,-18.1632446813081,
19.4732164465487));
#156909=CARTESIAN_POINT('Ctrl Pts',(-21.1437332452338,-18.0837602766129,
19.4773951243614));
#156910=CARTESIAN_POINT('Ctrl Pts',(-21.112686592475,-18.0057177509962,
19.4815738021741));
#156911=CARTESIAN_POINT('Ctrl Pts',(-21.0810834482228,-17.9262763627721,
19.4858273801273));
#156912=CARTESIAN_POINT('Ctrl Pts',(-21.0454603362217,-17.8483295278292,
19.4900809580806));
#156913=CARTESIAN_POINT('Ctrl Pts',(-21.0059873754064,-17.7723079359452,
19.4943345360339));
#156914=CARTESIAN_POINT('Ctrl Pts',(-20.967279678073,-17.697760176956,19.4985056497431));
#156915=CARTESIAN_POINT('Ctrl Pts',(-20.9248702958461,-17.6250641047766,
19.5026767634523));
#156916=CARTESIAN_POINT('Ctrl Pts',(-20.8789678617061,-17.5546049691487,
19.5068478771615));
#156917=CARTESIAN_POINT('Ctrl Pts',(-20.8330808305555,-17.4841694767402,
19.5110175912147));
#156918=CARTESIAN_POINT('Ctrl Pts',(-20.7837033262562,-17.4159698152611,
19.5151873052678));
#156919=CARTESIAN_POINT('Ctrl Pts',(-20.7310884046656,-17.3503639914293,
19.519357019321));
#156920=CARTESIAN_POINT('Ctrl Pts',(-20.6784753553166,-17.2847605021054,
19.5235265849996));
#156921=CARTESIAN_POINT('Ctrl Pts',(-20.6226254062025,-17.2217510252597,
19.5276961506783));
#156922=CARTESIAN_POINT('Ctrl Pts',(-20.5638323065115,-17.1616610013612,
19.5318657163569));
#156923=CARTESIAN_POINT('Ctrl Pts',(-20.5029721055919,-17.0994582777943,
19.5361818794149));
#156924=CARTESIAN_POINT('Ctrl Pts',(-20.4389583090022,-17.0403845006845,
19.5404980424729));
#156925=CARTESIAN_POINT('Ctrl Pts',(-20.3721573781207,-16.9847581733532,
19.5448142055309));
#156926=CARTESIAN_POINT('Ctrl Pts',(-20.3075324893086,-16.9309438750886,
19.5489897694644));
#156927=CARTESIAN_POINT('Ctrl Pts',(-20.2402996649794,-16.8803561190116,
19.553165333398));
#156928=CARTESIAN_POINT('Ctrl Pts',(-20.1708219663603,-16.8332403069284,
19.5573408973316));
#156929=CARTESIAN_POINT('Ctrl Pts',(-20.0978350997288,-16.7837447772679,
19.5617273599518));
#156930=CARTESIAN_POINT('Ctrl Pts',(-20.0223711203466,-16.738081448703,
19.566113822572));
#156931=CARTESIAN_POINT('Ctrl Pts',(-19.9448802162024,-16.6964803033426,
19.5705002851921));
#156932=CARTESIAN_POINT('Ctrl Pts',(-19.8673893120582,-16.6548791579822,
19.5748867478123));
#156933=CARTESIAN_POINT('Ctrl Pts',(-19.7878720403135,-16.6173403747379,
19.5792732104325));
#156934=CARTESIAN_POINT('Ctrl Pts',(-19.706800567316,-16.5840348279103,
19.5836596730527));
#156935=CARTESIAN_POINT('Ctrl Pts',(-19.6294593229195,-16.5522617227512,
19.587844307487));
#156936=CARTESIAN_POINT('Ctrl Pts',(-19.5504158778324,-16.5242225928466,
19.5920289419213));
#156937=CARTESIAN_POINT('Ctrl Pts',(-19.4700654949528,-16.500101228203,
19.5962135763556));
#156938=CARTESIAN_POINT('Ctrl Pts',(-19.3898294809444,-16.4760141973502,
19.6003922544784));
#156939=CARTESIAN_POINT('Ctrl Pts',(-19.3082906610536,-16.4558339863015,
19.6045709326011));
#156940=CARTESIAN_POINT('Ctrl Pts',(-19.2258642779044,-16.4396963694407,
19.6087496107238));
#156941=CARTESIAN_POINT('Ctrl Pts',(-19.1419604620519,-16.4232694975866,
19.6130031885992));
#156942=CARTESIAN_POINT('Ctrl Pts',(-19.0571373968203,-16.4110317555328,
19.6172567664746));
#156943=CARTESIAN_POINT('Ctrl Pts',(-18.9718493062316,-16.4030732243697,
19.6215103443501));
#156944=CARTESIAN_POINT('Ctrl Pts',(-18.8882146908572,-16.3952689847839,
19.6256814583605));
#156945=CARTESIAN_POINT('Ctrl Pts',(-18.8041333991978,-16.391579559832,
19.6298525723709));
#156946=CARTESIAN_POINT('Ctrl Pts',(-18.7200422944405,-16.3920380505844,
19.6340236863813));
#156947=CARTESIAN_POINT('Ctrl Pts',(-18.6359794073137,-16.3924963874856,
19.6381934007318));
#156948=CARTESIAN_POINT('Ctrl Pts',(-18.551907173272,-16.397099873298,19.6423631150822));
#156949=CARTESIAN_POINT('Ctrl Pts',(-18.4682635936936,-16.4058295103502,
19.6465328294327));
#156950=CARTESIAN_POINT('Ctrl Pts',(-18.3846229905612,-16.4145588367595,
19.6507023954044));
#156951=CARTESIAN_POINT('Ctrl Pts',(-18.3014114690234,-16.4274139738751,
19.6548719613761));
#156952=CARTESIAN_POINT('Ctrl Pts',(-18.2190616739277,-16.4443240798816,
19.6590415273478));
#156953=CARTESIAN_POINT('Ctrl Pts',(-18.1338165629824,-16.4618287240758,
19.6633576900466));
#156954=CARTESIAN_POINT('Ctrl Pts',(-18.0494954191543,-16.4836786817452,
19.6676738527455));
#156955=CARTESIAN_POINT('Ctrl Pts',(-17.9665644117748,-16.5097382167496,
19.6719900154444));
#156956=CARTESIAN_POINT('Ctrl Pts',(-17.8863348720819,-16.5349488655054,
19.6761655796575));
#156957=CARTESIAN_POINT('Ctrl Pts',(-17.8074067178225,-16.5640988419262,
19.6803411438706));
#156958=CARTESIAN_POINT('Ctrl Pts',(-17.7301828112974,-16.5970157003357,
19.6845167080837));
#156959=CARTESIAN_POINT('Ctrl Pts',(-17.6490585105613,-16.6315951102757,
19.6889031700254));
#156960=CARTESIAN_POINT('Ctrl Pts',(-17.5698156696774,-16.6703316765449,
19.6932896319672));
#156961=CARTESIAN_POINT('Ctrl Pts',(-17.4928913452169,-16.7129713474315,
19.6976760939089));
#156962=CARTESIAN_POINT('Ctrl Pts',(-17.4159670207564,-16.7556110183182,
19.7020625558507));
#156963=CARTESIAN_POINT('Ctrl Pts',(-17.3413616647363,-16.8021534221795,
19.7064490177924));
#156964=CARTESIAN_POINT('Ctrl Pts',(-17.2694745299275,-16.8522940330825,
19.7108354797342));
#156965=CARTESIAN_POINT('Ctrl Pts',(-17.2008950125392,-16.900127611461,
19.7150201150491));
#156966=CARTESIAN_POINT('Ctrl Pts',(-17.1345338099061,-16.9514136024644,
19.719204750364));
#156967=CARTESIAN_POINT('Ctrl Pts',(-17.0707594087139,-17.0059191343887,
19.7233893856789));
#156968=CARTESIAN_POINT('Ctrl Pts',(-17.0070757824026,-17.0603470845079,
19.727568064689));
#156969=CARTESIAN_POINT('Ctrl Pts',(-16.9459719906649,-17.1179851767066,
19.731746743699));
#156970=CARTESIAN_POINT('Ctrl Pts',(-16.8877869612783,-17.1785577495577,
19.7359254227091));
#156971=CARTESIAN_POINT('Ctrl Pts',(-16.8285590234002,-17.2402160252302,
19.7401790003636));
#156972=CARTESIAN_POINT('Ctrl Pts',(-16.7723559084922,-17.3049147399376,
19.744432578018));
#156973=CARTESIAN_POINT('Ctrl Pts',(-16.7194992231336,-17.3723207224235,
19.7486861556724));
#156974=CARTESIAN_POINT('Ctrl Pts',(-16.6676672533913,-17.4384199267333,
19.7528572705803));
#156975=CARTESIAN_POINT('Ctrl Pts',(-16.6190534156957,-17.5071219869974,
19.7570283854882));
#156976=CARTESIAN_POINT('Ctrl Pts',(-16.5739220086077,-17.5780774872276,
19.7611995003961));
#156977=CARTESIAN_POINT('Ctrl Pts',(-16.5288057458024,-17.6490091776496,
19.7653692156459));
#156978=CARTESIAN_POINT('Ctrl Pts',(-16.4871698395077,-17.722192418441,
19.7695389308956));
#156979=CARTESIAN_POINT('Ctrl Pts',(-16.4492353975645,-17.7972486365204,
19.7737086461453));
#156980=CARTESIAN_POINT('Ctrl Pts',(-16.4113023055078,-17.8723021837454,
19.7778782130169));
#156981=CARTESIAN_POINT('Ctrl Pts',(-16.3770706226668,-17.9492281647853,
19.7820477798885));
#156982=CARTESIAN_POINT('Ctrl Pts',(-16.3467149647707,-18.0276244483055,
19.7862173467601));
#156983=CARTESIAN_POINT('Ctrl Pts',(-16.3152920543962,-18.1087770096893,
19.790533508398));
#156984=CARTESIAN_POINT('Ctrl Pts',(-16.288022988789,-18.1915046955782,
19.794849670036));
#156985=CARTESIAN_POINT('Ctrl Pts',(-16.2650459638136,-18.2753420604184,
19.799165831674));
#156986=CARTESIAN_POINT('Ctrl Pts',(-16.2428174024766,-18.3564484703507,
19.8033413967792));
#156987=CARTESIAN_POINT('Ctrl Pts',(-16.2246056091634,-18.4385929047702,
19.8075169618844));
#156988=CARTESIAN_POINT('Ctrl Pts',(-16.2104836461321,-18.5213432785139,
19.8116925269897));
#156989=CARTESIAN_POINT('Ctrl Pts',(-16.1956484266957,-18.6082731161156,
19.816078986894));
#156990=CARTESIAN_POINT('Ctrl Pts',(-16.1853271121021,-18.6958711329071,
19.8204654467983));
#156991=CARTESIAN_POINT('Ctrl Pts',(-16.1795426555428,-18.7836323209494,
19.8248519067027));
#156992=CARTESIAN_POINT('Ctrl Pts',(-16.1737581989836,-18.8713935089917,
19.829238366607));
#156993=CARTESIAN_POINT('Ctrl Pts',(-16.1725105326347,-18.9593172870491,
19.8336248265113));
#156994=CARTESIAN_POINT('Ctrl Pts',(-16.1757597065439,-19.0469031134252,
19.8380112864157));
#156995=CARTESIAN_POINT('Ctrl Pts',(-16.1788596427641,-19.1304660383847,
19.8421962719891));
#156996=CARTESIAN_POINT('Ctrl Pts',(-16.1860639312553,-19.2140324391989,
19.8463812575626));
#156997=CARTESIAN_POINT('Ctrl Pts',(-16.1973762176809,-19.2971663178426,
19.850566243136));
#156998=CARTESIAN_POINT('Ctrl Pts',(-16.208669157137,-19.3801580158035,
19.8547440712892));
#156999=CARTESIAN_POINT('Ctrl Pts',(-16.2240560627403,-19.4627182105596,
19.8589218994425));
#157000=CARTESIAN_POINT('Ctrl Pts',(-16.2434886326561,-19.5444129717781,
19.8630997275957));
#157001=CARTESIAN_POINT('Ctrl Pts',(-16.2629022923872,-19.6260282343488,
19.8672734902288));
#157002=CARTESIAN_POINT('Ctrl Pts',(-16.2863536946398,-19.7067792904715,
19.871447252862));
#157003=CARTESIAN_POINT('Ctrl Pts',(-16.3137431277316,-19.7862401765904,
19.8756210154952));
#157004=CARTESIAN_POINT('Ctrl Pts',(-16.3411141246999,-19.865647576728,
19.8797919687236));
#157005=CARTESIAN_POINT('Ctrl Pts',(-16.3724177386845,-19.9437660979487,
19.8839629219521));
#157006=CARTESIAN_POINT('Ctrl Pts',(-16.4075041942595,-20.0201840973689,
19.8881338751805));
#157007=CARTESIAN_POINT('Ctrl Pts',(-16.4425775582141,-20.0965735833524,
19.8923032721236));
#157008=CARTESIAN_POINT('Ctrl Pts',(-16.4814307670068,-20.1712633909202,
19.8964726690667));
#157009=CARTESIAN_POINT('Ctrl Pts',(-16.5238661301382,-20.2438623290775,
19.9006420660098));
#157010=CARTESIAN_POINT('Ctrl Pts',(-16.5663181358782,-20.3164897396133,
19.9048130981373));
#157011=CARTESIAN_POINT('Ctrl Pts',(-16.612354878163,-20.3870242402789,
19.9089841302648));
#157012=CARTESIAN_POINT('Ctrl Pts',(-16.661733317948,-20.4551003953353,
19.9131551623922));
#157013=CARTESIAN_POINT('Ctrl Pts',(-16.7111193613354,-20.5231870331858,
19.9173268368015));
#157014=CARTESIAN_POINT('Ctrl Pts',(-16.7638478466874,-20.5888142060546,
19.9214985112107));
#157015=CARTESIAN_POINT('Ctrl Pts',(-16.8196343574744,-20.6516482538212,
19.9256701856199));
#157016=CARTESIAN_POINT('Ctrl Pts',(-16.8754895074255,-20.7145596119709,
19.9298469928155));
#157017=CARTESIAN_POINT('Ctrl Pts',(-16.9344098847018,-20.774670642438,
19.9340238000111));
#157018=CARTESIAN_POINT('Ctrl Pts',(-16.9960732526694,-20.8316836491582,
19.9382006072068));
#157019=CARTESIAN_POINT('Ctrl Pts',(-17.0532712047221,-20.8845680006338,
19.9420749466336));
#157020=CARTESIAN_POINT('Ctrl Pts',(-17.1128286535666,-20.9347869850788,
19.9459492860605));
#157021=CARTESIAN_POINT('Ctrl Pts',(-17.1744641402401,-20.9821349467765,
19.9498236254873));
#157022=CARTESIAN_POINT('Ctrl Pts',(-17.1767158074852,-20.9792339848999,
19.149828714141));
#157023=CARTESIAN_POINT('Ctrl Pts',(-17.4546312945708,-21.1947985643844,
19.1672632270968));
#157024=CARTESIAN_POINT('Ctrl Pts',(-18.5512406568725,-21.7455419441639,
19.2270896756131));
#157025=CARTESIAN_POINT('Ctrl Pts',(-20.6359183918341,-21.202775782827,
19.3215765970986));
#157026=CARTESIAN_POINT('Ctrl Pts',(-21.2889868109407,-19.6455867711505,
19.3986290056282));
#157027=CARTESIAN_POINT('Ctrl Pts',(-21.2953147898194,-18.9498155448408,
19.4332894785973));
#157028=CARTESIAN_POINT('',(-21.2939989850553,-18.9542795868244,19.3667098901939));
#157029=CARTESIAN_POINT('Ctrl Pts',(-17.1744641402401,-20.9821349467764,
19.0833436902736));
#157030=CARTESIAN_POINT('Ctrl Pts',(-17.2408452334434,-21.0331284511368,
19.0875248451816));
#157031=CARTESIAN_POINT('Ctrl Pts',(-17.3098396878856,-21.080946991935,
19.0917060000897));
#157032=CARTESIAN_POINT('Ctrl Pts',(-17.3811105272675,-21.1253131561212,
19.0958871549977));
#157033=CARTESIAN_POINT('Ctrl Pts',(-17.4522930341336,-21.1696243332337,
19.1000631278153));
#157034=CARTESIAN_POINT('Ctrl Pts',(-17.5257459330175,-21.2104913926985,
19.1042391006329));
#157035=CARTESIAN_POINT('Ctrl Pts',(-17.6011009621195,-21.2476784988254,
19.1084150734506));
#157036=CARTESIAN_POINT('Ctrl Pts',(-17.6763877017987,-21.2848319046666,
19.1125872618523));
#157037=CARTESIAN_POINT('Ctrl Pts',(-17.7535727350803,-21.3183117817329,
19.116759450254));
#157038=CARTESIAN_POINT('Ctrl Pts',(-17.8322618834364,-21.3479274548985,
19.1209316386556));
#157039=CARTESIAN_POINT('Ctrl Pts',(-17.9109136780137,-21.3775290694889,
19.1251018465174));
#157040=CARTESIAN_POINT('Ctrl Pts',(-17.9910677400756,-21.4032699606739,
19.1292720543791));
#157041=CARTESIAN_POINT('Ctrl Pts',(-18.0723096286257,-21.4250074509452,
19.1334422622408));
#157042=CARTESIAN_POINT('Ctrl Pts',(-18.15353732237,-21.4467411431826,19.1376117414724));
#157043=CARTESIAN_POINT('Ctrl Pts',(-18.2358520206424,-21.4644727055195,
19.141781220704));
#157044=CARTESIAN_POINT('Ctrl Pts',(-18.3188251471571,-21.4781096258015,
19.1459506999355));
#157045=CARTESIAN_POINT('Ctrl Pts',(-18.4018086660397,-21.4917482541051,
19.1501207013936));
#157046=CARTESIAN_POINT('Ctrl Pts',(-18.4854503227753,-21.50129114871,19.1542907028516));
#157047=CARTESIAN_POINT('Ctrl Pts',(-18.5693137603081,-21.5066973289328,
19.1584607043096));
#157048=CARTESIAN_POINT('Ctrl Pts',(-18.6532674185104,-21.5121093251489,
19.1626351918743));
#157049=CARTESIAN_POINT('Ctrl Pts',(-18.7374428738953,-21.5133756933231,
19.1668096794389));
#157050=CARTESIAN_POINT('Ctrl Pts',(-18.821401611171,-21.5105075646487,
19.1709841670036));
#157051=CARTESIAN_POINT('Ctrl Pts',(-18.9054094707161,-21.5076377579002,
19.1751610969621));
#157052=CARTESIAN_POINT('Ctrl Pts',(-18.9891999013505,-21.5006286769763,
19.1793380269206));
#157053=CARTESIAN_POINT('Ctrl Pts',(-19.0723397717153,-21.4895433393098,
19.1835149568791));
#157054=CARTESIAN_POINT('Ctrl Pts',(-19.1556200492609,-21.4784392806494,
19.1876989408654));
#157055=CARTESIAN_POINT('Ctrl Pts',(-19.2382471205611,-21.4632453034702,
19.1918829248517));
#157056=CARTESIAN_POINT('Ctrl Pts',(-19.3197986310449,-21.4440754330208,
19.1960669088381));
#157057=CARTESIAN_POINT('Ctrl Pts',(-19.3683964228494,-21.4326518141634,
19.1985602088576));
#157058=CARTESIAN_POINT('Ctrl Pts',(-19.4166125476408,-21.4198172577591,
19.2010535088771));
#157059=CARTESIAN_POINT('Ctrl Pts',(-19.4643607861739,-21.4056041086572,
19.2035468088966));
#157060=CARTESIAN_POINT('Ctrl Pts',(-19.5444991251693,-21.3817494451991,
19.2077314433108));
#157061=CARTESIAN_POINT('Ctrl Pts',(-19.6236166763929,-21.3539201055357,
19.211916077725));
#157062=CARTESIAN_POINT('Ctrl Pts',(-19.7012904348026,-21.3222213429846,
19.2161007121391));
#157063=CARTESIAN_POINT('Ctrl Pts',(-19.778853634233,-21.2905676996977,
19.2202793902443));
#157064=CARTESIAN_POINT('Ctrl Pts',(-19.8549767005595,-21.2550557457739,
19.2244580683494));
#157065=CARTESIAN_POINT('Ctrl Pts',(-19.9292512406756,-21.215840646261,
19.2286367464546));
#157066=CARTESIAN_POINT('Ctrl Pts',(-20.0048570980657,-21.1759226445248,
19.2328903243347));
#157067=CARTESIAN_POINT('Ctrl Pts',(-20.0785470456786,-21.1321675712325,
19.2371439022148));
#157068=CARTESIAN_POINT('Ctrl Pts',(-20.1499110579027,-21.0847906311002,
19.241397480095));
#157069=CARTESIAN_POINT('Ctrl Pts',(-20.2198915399371,-21.038332185107,
19.2455685940941));
#157070=CARTESIAN_POINT('Ctrl Pts',(-20.2876350664325,-20.9883913190918,
19.2497397080933));
#157071=CARTESIAN_POINT('Ctrl Pts',(-20.3527809100999,-20.935216671243,
19.2539108220924));
#157072=CARTESIAN_POINT('Ctrl Pts',(-20.4179048934498,-20.8820598666613,
19.2580805364339));
#157073=CARTESIAN_POINT('Ctrl Pts',(-20.480432569049,-20.8256717259784,
19.2622502507755));
#157074=CARTESIAN_POINT('Ctrl Pts',(-20.5400350473299,-20.766342141884,
19.266419965117));
#157075=CARTESIAN_POINT('Ctrl Pts',(-20.5996354046978,-20.7070146689917,
19.2705895310821));
#157076=CARTESIAN_POINT('Ctrl Pts',(-20.6563104462706,-20.6447462859464,
19.2747590970472));
#157077=CARTESIAN_POINT('Ctrl Pts',(-20.709768014027,-20.5798638624738,
19.2789286630123));
#157078=CARTESIAN_POINT('Ctrl Pts',(-20.7651050833169,-20.5127002537633,
19.2832448257261));
#157079=CARTESIAN_POINT('Ctrl Pts',(-20.8169938810792,-20.4427357722886,
19.2875609884399));
#157080=CARTESIAN_POINT('Ctrl Pts',(-20.8651569232063,-20.3703688408415,
19.2918771511538));
#157081=CARTESIAN_POINT('Ctrl Pts',(-20.9117510598039,-20.3003592538204,
19.2960527153661));
#157082=CARTESIAN_POINT('Ctrl Pts',(-20.9548582452865,-20.2281017614681,
19.3002282795785));
#157083=CARTESIAN_POINT('Ctrl Pts',(-20.9942733140312,-20.1539835880237,
19.3044038437908));
#157084=CARTESIAN_POINT('Ctrl Pts',(-21.0356791435395,-20.0761218830757,
19.3087903057554));
#157085=CARTESIAN_POINT('Ctrl Pts',(-21.0730098296578,-19.9962071202703,
19.3131767677199));
#157086=CARTESIAN_POINT('Ctrl Pts',(-21.1060848561741,-19.9147115014943,
19.3175632296844));
#157087=CARTESIAN_POINT('Ctrl Pts',(-21.1391598826905,-19.8332158827183,
19.321949691649));
#157088=CARTESIAN_POINT('Ctrl Pts',(-21.1679791313071,-19.7501399810715,
19.3263361536135));
#157089=CARTESIAN_POINT('Ctrl Pts',(-21.1924232051046,-19.6659715292665,
19.330722615578));
#157090=CARTESIAN_POINT('Ctrl Pts',(-21.2214742546437,-19.56593984538,19.3359357942359));
#157091=CARTESIAN_POINT('Ctrl Pts',(-21.2444357643464,-19.4640653478474,
19.3411489728938));
#157092=CARTESIAN_POINT('Ctrl Pts',(-21.261115150052,-19.3610098023001,
19.3463621515516));
#157093=CARTESIAN_POINT('Ctrl Pts',(-21.277528721009,-19.2595966244285,
19.3514922492257));
#157094=CARTESIAN_POINT('Ctrl Pts',(-21.2878587862943,-19.1570396545895,
19.3566223468997));
#157095=CARTESIAN_POINT('Ctrl Pts',(-21.2919675308073,-19.0539907414198,
19.3617524445737));
#157096=CARTESIAN_POINT('Ctrl Pts',(-21.2932910194155,-19.020797131491,
19.3634049264471));
#157097=CARTESIAN_POINT('Ctrl Pts',(-21.2939693565913,-18.9875526505269,
19.3650574083205));
#157098=CARTESIAN_POINT('Ctrl Pts',(-21.2939989850553,-18.9542795868244,
19.3667098901939));
#157099=CARTESIAN_POINT('Ctrl Pts',(-21.2939989850559,-18.954279586128,
19.3667098902285));
#157100=CARTESIAN_POINT('Ctrl Pts',(-21.294073180434,-18.8709574030256,
19.3708480242597));
#157101=CARTESIAN_POINT('Ctrl Pts',(-21.2900751830219,-18.7875513930813,
19.3749861582908));
#157102=CARTESIAN_POINT('Ctrl Pts',(-21.2820071809341,-18.7044936245096,
19.379124292322));
#157103=CARTESIAN_POINT('Ctrl Pts',(-21.2739428344709,-18.6214734895453,
19.3832605513581));
#157104=CARTESIAN_POINT('Ctrl Pts',(-21.2618121886764,-18.5388017480938,
19.3873968103941));
#157105=CARTESIAN_POINT('Ctrl Pts',(-21.2456694473266,-18.4569074961523,
19.3915330694301));
#157106=CARTESIAN_POINT('Ctrl Pts',(-21.2295289836496,-18.3750247991451,
19.3956687448574));
#157107=CARTESIAN_POINT('Ctrl Pts',(-21.2093776397613,-18.2939198329769,
19.3998044202847));
#157108=CARTESIAN_POINT('Ctrl Pts',(-21.1853208566141,-18.214012155975,
19.403940095712));
#157109=CARTESIAN_POINT('Ctrl Pts',(-21.1612599617833,-18.1340908214908,
19.4080764779915));
#157110=CARTESIAN_POINT('Ctrl Pts',(-21.1332924395156,-18.0553676300856,
19.4122128602709));
#157111=CARTESIAN_POINT('Ctrl Pts',(-21.1015733410968,-17.9782461940883,
19.4163492425504));
#157112=CARTESIAN_POINT('Ctrl Pts',(-21.0698191717564,-17.901039487072,
19.4204901983123));
#157113=CARTESIAN_POINT('Ctrl Pts',(-21.0343053289603,-17.825438502363,
19.4246311540741));
#157114=CARTESIAN_POINT('Ctrl Pts',(-20.9952344193641,-17.7518254707406,
19.428772109836));
#157115=CARTESIAN_POINT('Ctrl Pts',(-20.9561382227283,-17.6781647961105,
19.4329157456612));
#157116=CARTESIAN_POINT('Ctrl Pts',(-20.9134806196083,-17.6064950352479,
19.4370593814864));
#157117=CARTESIAN_POINT('Ctrl Pts',(-20.8675081508587,-17.5371703387972,
19.4412030173116));
#157118=CARTESIAN_POINT('Ctrl Pts',(-20.8214607545949,-17.4677326545666,
19.4453534065774));
#157119=CARTESIAN_POINT('Ctrl Pts',(-20.7720879921757,-17.4006480348511,
19.4495037958431));
#157120=CARTESIAN_POINT('Ctrl Pts',(-20.7196769297237,-17.3362379102222,
19.4536541851088));
#157121=CARTESIAN_POINT('Ctrl Pts',(-20.7018115389434,-17.3142823918094,
19.4550689308257));
#157122=CARTESIAN_POINT('Ctrl Pts',(-20.6835934338648,-17.2926373126042,
19.4564836765426));
#157123=CARTESIAN_POINT('Ctrl Pts',(-20.6650349200515,-17.2713143846806,
19.4578984222595));
#157124=CARTESIAN_POINT('Ctrl Pts',(-20.6101412425931,-17.2082439287333,
19.4620830566462));
#157125=CARTESIAN_POINT('Ctrl Pts',(-20.552052199416,-17.1477482923966,
19.4662676910329));
#157126=CARTESIAN_POINT('Ctrl Pts',(-20.4910387353975,-17.0901689436706,
19.4704523254196));
#157127=CARTESIAN_POINT('Ctrl Pts',(-20.4301121164985,-17.0326715520257,
19.4746310034968));
#157128=CARTESIAN_POINT('Ctrl Pts',(-20.3662696766049,-16.9780825158894,
19.4788096815741));
#157129=CARTESIAN_POINT('Ctrl Pts',(-20.2998217436397,-16.9267093376147,
19.4829883596513));
#157130=CARTESIAN_POINT('Ctrl Pts',(-20.2321827790971,-16.8744153319368,
19.4872419375384));
#157131=CARTESIAN_POINT('Ctrl Pts',(-20.1618443123322,-16.8254539702931,
19.4914955154255));
#157132=CARTESIAN_POINT('Ctrl Pts',(-20.0891719990944,-16.7801093828486,
19.4957490933125));
#157133=CARTESIAN_POINT('Ctrl Pts',(-20.0179085806131,-16.7356438888117,
19.4999202072829));
#157134=CARTESIAN_POINT('Ctrl Pts',(-19.9444014087305,-16.6946564386937,
19.5040913212534));
#157135=CARTESIAN_POINT('Ctrl Pts',(-19.8690261614839,-16.6573724457448,
19.5082624352238));
#157136=CARTESIAN_POINT('Ctrl Pts',(-19.7936762071349,-16.6201009638025,
19.5124321495363));
#157137=CARTESIAN_POINT('Ctrl Pts',(-19.7164598343598,-16.5865306747405,
19.5166018638488));
#157138=CARTESIAN_POINT('Ctrl Pts',(-19.6377770918967,-16.5568409305095,
19.5207715781614));
#157139=CARTESIAN_POINT('Ctrl Pts',(-19.5590971493085,-16.527152242769,
19.5249411440973));
#157140=CARTESIAN_POINT('Ctrl Pts',(-19.4789513714909,-16.5013439869193,
19.5291107100332));
#157141=CARTESIAN_POINT('Ctrl Pts',(-19.3977582580731,-16.4795467699389,
19.5332802759692));
#157142=CARTESIAN_POINT('Ctrl Pts',(-19.3137104946165,-16.4569831896096,
19.5375964387168));
#157143=CARTESIAN_POINT('Ctrl Pts',(-19.2285408859958,-16.4387180891116,
19.5419126014644));
#157144=CARTESIAN_POINT('Ctrl Pts',(-19.1427269885612,-16.4248390932072,
19.5462287642121));
#157145=CARTESIAN_POINT('Ctrl Pts',(-19.0597084701507,-16.4114122041898,
19.5504043283951));
#157146=CARTESIAN_POINT('Ctrl Pts',(-18.9760874671123,-16.4020900585603,
19.554579892578));
#157147=CARTESIAN_POINT('Ctrl Pts',(-18.8923014001436,-16.3968990887418,
19.558755456761));
#157148=CARTESIAN_POINT('Ctrl Pts',(-18.8042834975808,-16.391445935345,
19.5631419187909));
#157149=CARTESIAN_POINT('Ctrl Pts',(-18.7160840019592,-16.3905522627805,
19.5675283808209));
#157150=CARTESIAN_POINT('Ctrl Pts',(-18.6282074804617,-16.3941868827434,
19.5719148428509));
#157151=CARTESIAN_POINT('Ctrl Pts',(-18.5403309589642,-16.3978215027064,
19.5763013048809));
#157152=CARTESIAN_POINT('Ctrl Pts',(-18.4527779822414,-16.4059842855988,
19.5806877669109));
#157153=CARTESIAN_POINT('Ctrl Pts',(-18.3660419494154,-16.4185819782338,
19.5850742289409));
#157154=CARTESIAN_POINT('Ctrl Pts',(-18.2832967675646,-16.4306000327149,
19.5892588634754));
#157155=CARTESIAN_POINT('Ctrl Pts',(-18.2009870107893,-16.4466985853957,
19.59344349801));
#157156=CARTESIAN_POINT('Ctrl Pts',(-18.1195464569871,-16.4668346446405,
19.5976281325445));
#157157=CARTESIAN_POINT('Ctrl Pts',(-18.0382218237187,-16.4869420427009,
19.6018068107705));
#157158=CARTESIAN_POINT('Ctrl Pts',(-17.9577643787149,-16.5110754227199,
19.6059854889965));
#157159=CARTESIAN_POINT('Ctrl Pts',(-17.878600657432,-16.5391402931927,
19.6101641672224));
#157160=CARTESIAN_POINT('Ctrl Pts',(-17.7980179867494,-16.5677082050898,
19.6144177450724));
#157161=CARTESIAN_POINT('Ctrl Pts',(-17.7187763529939,-16.6003498680467,
19.6186713229224));
#157162=CARTESIAN_POINT('Ctrl Pts',(-17.6413125871542,-16.6369116177112,
19.6229249007724));
#157163=CARTESIAN_POINT('Ctrl Pts',(-17.5653506043487,-16.6727645480362,
19.6270960148927));
#157164=CARTESIAN_POINT('Ctrl Pts',(-17.4910986050711,-16.712386719325,
19.631267129013));
#157165=CARTESIAN_POINT('Ctrl Pts',(-17.4189494736076,-16.7555842576973,
19.6354382431332));
#157166=CARTESIAN_POINT('Ctrl Pts',(-17.3468245524847,-16.7987673007169,
19.6396079575957));
#157167=CARTESIAN_POINT('Ctrl Pts',(-17.2768014921365,-16.845523091981,
19.6437776720582));
#157168=CARTESIAN_POINT('Ctrl Pts',(-17.2092476379827,-16.8956123335999,
19.6479473865207));
#157169=CARTESIAN_POINT('Ctrl Pts',(-17.141696187691,-16.9456997928241,
19.6521169526065));
#157170=CARTESIAN_POINT('Ctrl Pts',(-17.0766141379211,-16.9991201918754,
19.6562865186922));
#157171=CARTESIAN_POINT('Ctrl Pts',(-17.0143378344021,-17.0555923338556,
19.660456084778));
#157172=CARTESIAN_POINT('Ctrl Pts',(-16.9498719775865,-17.1140499624118,
19.6647722473484));
#157173=CARTESIAN_POINT('Ctrl Pts',(-16.8884132283207,-17.1757775704978,
19.6690884099187));
#157174=CARTESIAN_POINT('Ctrl Pts',(-16.8302937573018,-17.2404210384818,
19.6734045724891));
#157175=CARTESIAN_POINT('Ctrl Pts',(-16.7740675178662,-17.3029587568246,
19.6775801368201));
#157176=CARTESIAN_POINT('Ctrl Pts',(-16.7209666047403,-17.3682248893115,
19.6817557011511));
#157177=CARTESIAN_POINT('Ctrl Pts',(-16.6712500109568,-17.4358659417115,
19.6859312654821));
#157178=CARTESIAN_POINT('Ctrl Pts',(-16.6190223557939,-17.5069233752716,
19.6903177271722));
#157179=CARTESIAN_POINT('Ctrl Pts',(-16.5705302089911,-17.5806014599345,
19.6947041888622));
#157180=CARTESIAN_POINT('Ctrl Pts',(-16.5260204587108,-17.6564590530407,
19.6990906505522));
#157181=CARTESIAN_POINT('Ctrl Pts',(-16.4815107084305,-17.7323166461468,
19.7034771122423));
#157182=CARTESIAN_POINT('Ctrl Pts',(-16.4409835545834,-17.810353197721,
19.7078635739323));
#157183=CARTESIAN_POINT('Ctrl Pts',(-16.4046276535563,-17.8901033611394,
19.7122500356223));
#157184=CARTESIAN_POINT('Ctrl Pts',(-16.3699445411289,-17.9661841019766,
19.7164346697438));
#157185=CARTESIAN_POINT('Ctrl Pts',(-16.3389281684892,-18.0441074153348,
19.7206193038652));
#157186=CARTESIAN_POINT('Ctrl Pts',(-16.3117771822314,-18.1234852921757,
19.7248039379867));
#157187=CARTESIAN_POINT('Ctrl Pts',(-16.2846648420429,-18.2027501844311,
19.7289826157992));
#157188=CARTESIAN_POINT('Ctrl Pts',(-16.2614071073441,-18.2834650961696,
19.7331612936118));
#157189=CARTESIAN_POINT('Ctrl Pts',(-16.2421554012958,-18.3652202321922,
19.7373399714244));
#157190=CARTESIAN_POINT('Ctrl Pts',(-16.2225586206672,-18.4484407770037,
19.7415935493777));
#157191=CARTESIAN_POINT('Ctrl Pts',(-16.207113098083,-18.5327387664133,
19.745847127331));
#157192=CARTESIAN_POINT('Ctrl Pts',(-16.1959260745188,-18.617663719001,
19.7501007052843));
#157193=CARTESIAN_POINT('Ctrl Pts',(-16.1849559341181,-18.7009422289687,
19.7542718189934));
#157194=CARTESIAN_POINT('Ctrl Pts',(-16.1780807097886,-18.7848231320472,
19.7584429327025));
#157195=CARTESIAN_POINT('Ctrl Pts',(-16.1753500450965,-18.8688711345423,
19.7626140464116));
#157196=CARTESIAN_POINT('Ctrl Pts',(-16.1726202967043,-18.9528909339471,
19.7667837604647));
#157197=CARTESIAN_POINT('Ctrl Pts',(-16.1740323608325,-19.0370772620015,
19.7709534745177));
#157198=CARTESIAN_POINT('Ctrl Pts',(-16.1795838629395,-19.1209917120006,
19.7751231885707));
#157199=CARTESIAN_POINT('Ctrl Pts',(-16.1851351675026,-19.2049031760005,
19.7792927542493));
#157200=CARTESIAN_POINT('Ctrl Pts',(-16.1948255859618,-19.2885423222071,
19.7834623199278));
#157201=CARTESIAN_POINT('Ctrl Pts',(-16.2086007337952,-19.3714741306115,
19.7876318856064));
#157202=CARTESIAN_POINT('Ctrl Pts',(-16.2228602007955,-19.457321730907,
19.7919480486645));
#157203=CARTESIAN_POINT('Ctrl Pts',(-16.2414968944622,-19.5424108074415,
19.7962642117226));
#157204=CARTESIAN_POINT('Ctrl Pts',(-16.26439285385,-19.6262703787688,19.8005803747807));
#157205=CARTESIAN_POINT('Ctrl Pts',(-16.2865429767612,-19.7073982223639,
19.8047559387142));
#157206=CARTESIAN_POINT('Ctrl Pts',(-16.3126789433259,-19.7873750001408,
19.8089315026477));
#157207=CARTESIAN_POINT('Ctrl Pts',(-16.34264370885,-19.8657916002993,19.8131070665811));
#157208=CARTESIAN_POINT('Ctrl Pts',(-16.3741219297554,-19.9481688530246,
19.8174935292016));
#157209=CARTESIAN_POINT('Ctrl Pts',(-16.4098256651424,-20.0288236423437,
19.821879991822));
#157210=CARTESIAN_POINT('Ctrl Pts',(-16.4495176194985,-20.1073095919183,
19.8262664544425));
#157211=CARTESIAN_POINT('Ctrl Pts',(-16.4892095738547,-20.1857955414929,
19.8306529170629));
#157212=CARTESIAN_POINT('Ctrl Pts',(-16.532889392945,-20.2621121855376,
19.8350393796833));
#157213=CARTESIAN_POINT('Ctrl Pts',(-16.5802679097415,-20.3358490103298,
19.8394258423038));
#157214=CARTESIAN_POINT('Ctrl Pts',(-16.6254567089947,-20.4061779019541,
19.8436095735007));
#157215=CARTESIAN_POINT('Ctrl Pts',(-16.6741780301271,-20.4744218961067,
19.8477933046977));
#157216=CARTESIAN_POINT('Ctrl Pts',(-16.726213289138,-20.5402041819885,
19.8519770358946));
#157217=CARTESIAN_POINT('Ctrl Pts',(-16.7781836605675,-20.6059044378486,
19.8561555500099));
#157218=CARTESIAN_POINT('Ctrl Pts',(-16.8334594864442,-20.669148719787,
19.8603340641251));
#157219=CARTESIAN_POINT('Ctrl Pts',(-16.8917781973807,-20.729587924676,
19.8645125782403));
#157220=CARTESIAN_POINT('Ctrl Pts',(-16.9500311212365,-20.7899589504372,
19.8686863787355));
#157221=CARTESIAN_POINT('Ctrl Pts',(-17.0113197908613,-20.8475308583887,
19.8728601792307));
#157222=CARTESIAN_POINT('Ctrl Pts',(-17.0753415571519,-20.9019877358508,
19.8770339797259));
#157223=CARTESIAN_POINT('Ctrl Pts',(-17.1076991188394,-20.9295110591499,
19.8791434811473));
#157224=CARTESIAN_POINT('Ctrl Pts',(-17.1407542103651,-20.9562392078978,
19.8812529825688));
#157225=CARTESIAN_POINT('Ctrl Pts',(-17.1744641402401,-20.9821349467765,
19.8833624839903));
#157226=CARTESIAN_POINT('Origin',(-18.734,-18.952,-1.76670989022851));
#157227=CARTESIAN_POINT('',(-17.1744641402402,-20.9821349467765,20.7499611383185));
#157228=CARTESIAN_POINT('',(-17.1763037530772,-20.9797762769265,20.6832232033274));
#157229=CARTESIAN_POINT('',(-17.1744641402401,-20.9821349467765,-1.76670989022851));
#157230=CARTESIAN_POINT('',(-21.2939995273704,-18.9535555909848,20.2332901098006));
#157231=CARTESIAN_POINT('Ctrl Pts',(-21.2939995273704,-18.9535555909848,
20.2332901098006));
#157232=CARTESIAN_POINT('Ctrl Pts',(-21.294049723898,-18.870948345104,20.2374173417263));
#157233=CARTESIAN_POINT('Ctrl Pts',(-21.2900972917066,-18.7881812203374,
20.241544573652));
#157234=CARTESIAN_POINT('Ctrl Pts',(-21.2821221997477,-18.7056805830778,
20.2456718055777));
#157235=CARTESIAN_POINT('Ctrl Pts',(-21.2739869562085,-18.6215232116386,
20.2498819183928));
#157236=CARTESIAN_POINT('Ctrl Pts',(-21.2616656480612,-18.537643639815,
20.254092031208));
#157237=CARTESIAN_POINT('Ctrl Pts',(-21.2451929664636,-18.4544963465625,
20.2583021440231));
#157238=CARTESIAN_POINT('Ctrl Pts',(-21.229080068103,-18.3731650904946,
20.2624203028958));
#157239=CARTESIAN_POINT('Ctrl Pts',(-21.2089953895162,-18.2925349412607,
20.2665384617684));
#157240=CARTESIAN_POINT('Ctrl Pts',(-21.1850236976428,-18.2130258234598,
20.270656620641));
#157241=CARTESIAN_POINT('Ctrl Pts',(-21.1610629749352,-18.1335530881012,
20.2747728950923));
#157242=CARTESIAN_POINT('Ctrl Pts',(-21.1332189046361,-18.055200818656,
20.2788891695437));
#157243=CARTESIAN_POINT('Ctrl Pts',(-21.1016267121137,-17.9783759698499,
20.283005443995));
#157244=CARTESIAN_POINT('Ctrl Pts',(-21.0700389130291,-17.9015618048605,
20.2871211460075));
#157245=CARTESIAN_POINT('Ctrl Pts',(-21.0347042074052,-17.8262750760015,
20.2912368480201));
#157246=CARTESIAN_POINT('Ctrl Pts',(-20.9958062193322,-17.752903412485,
20.2953525500326));
#157247=CARTESIAN_POINT('Ctrl Pts',(-20.9553538853537,-17.6765998506772,
20.299632713625));
#157248=CARTESIAN_POINT('Ctrl Pts',(-20.9110477424172,-17.6023681210458,
20.3039128772174));
#157249=CARTESIAN_POINT('Ctrl Pts',(-20.8631463424907,-17.5306148121433,
20.3081930408098));
#157250=CARTESIAN_POINT('Ctrl Pts',(-20.817026382064,-17.4615299884816,
20.3123140263301));
#157251=CARTESIAN_POINT('Ctrl Pts',(-20.767574190865,-17.394742855338,20.3164350118505));
#157252=CARTESIAN_POINT('Ctrl Pts',(-20.7150628530422,-17.3305839607626,
20.3205559973708));
#157253=CARTESIAN_POINT('Ctrl Pts',(-20.6625158707606,-17.2663815154195,
20.3246797801975));
#157254=CARTESIAN_POINT('Ctrl Pts',(-20.6069059305284,-17.204811205117,
20.3288035630242));
#157255=CARTESIAN_POINT('Ctrl Pts',(-20.5485433980296,-17.1461671570527,
20.3329273458509));
#157256=CARTESIAN_POINT('Ctrl Pts',(-20.4900913111083,-17.0874331225942,
20.3370574564186));
#157257=CARTESIAN_POINT('Ctrl Pts',(-20.4288785613994,-17.031634616857,
20.3411875669862));
#157258=CARTESIAN_POINT('Ctrl Pts',(-20.3652483132487,-16.9790253573542,
20.3453176775539));
#157259=CARTESIAN_POINT('Ctrl Pts',(-20.3580748979454,-16.9730944034733,
20.3457832894164));
#157260=CARTESIAN_POINT('Ctrl Pts',(-20.3508707868094,-16.9672039368768,
20.3462489012788));
#157261=CARTESIAN_POINT('Ctrl Pts',(-20.3436364930174,-16.961354285578,
20.3467145131413));
#157262=CARTESIAN_POINT('Ctrl Pts',(-20.2786189220457,-16.9087810656599,
20.3508991582751));
#157263=CARTESIAN_POINT('Ctrl Pts',(-20.2109019646558,-16.8592987216113,
20.3550838034089));
#157264=CARTESIAN_POINT('Ctrl Pts',(-20.1408117772448,-16.813196450488,
20.3592684485427));
#157265=CARTESIAN_POINT('Ctrl Pts',(-20.0708213560678,-16.7671598012461,
20.3634471372609));
#157266=CARTESIAN_POINT('Ctrl Pts',(-19.9984647957972,-16.724493919034,
20.3676258259791));
#157267=CARTESIAN_POINT('Ctrl Pts',(-19.9241011351325,-16.6854477089297,
20.3718045146973));
#157268=CARTESIAN_POINT('Ctrl Pts',(-19.8484047994816,-16.6457017496864,
20.3760580899108));
#157269=CARTESIAN_POINT('Ctrl Pts',(-19.7706290892635,-16.6097067834814,
20.3803116651244));
#157270=CARTESIAN_POINT('Ctrl Pts',(-19.6911834645766,-16.5776790833712,
20.384565240338));
#157271=CARTESIAN_POINT('Ctrl Pts',(-19.6132778070226,-16.5462722054359,
20.3887363646167));
#157272=CARTESIAN_POINT('Ctrl Pts',(-19.5337668426417,-16.5186803435126,
20.3929074888954));
#157273=CARTESIAN_POINT('Ctrl Pts',(-19.4530597028474,-16.4950602075466,
20.3970786131741));
#157274=CARTESIAN_POINT('Ctrl Pts',(-19.3723796478629,-16.47144799835,20.4012483376496));
#157275=CARTESIAN_POINT('Ctrl Pts',(-19.2905046558528,-16.4518049970839,
20.4054180621252));
#157276=CARTESIAN_POINT('Ctrl Pts',(-19.2078598549769,-16.4362383185522,
20.4095877866007));
#157277=CARTESIAN_POINT('Ctrl Pts',(-19.1252179980804,-16.4206721945378,
20.4137573625421));
#157278=CARTESIAN_POINT('Ctrl Pts',(-19.0418068390792,-16.4091821888638,
20.4179269384834));
#157279=CARTESIAN_POINT('Ctrl Pts',(-18.9580612068526,-16.4018242069254,
20.4220965144247));
#157280=CARTESIAN_POINT('Ctrl Pts',(-18.8713716361879,-16.3942075673677,
20.4264126648745));
#157281=CARTESIAN_POINT('Ctrl Pts',(-18.7843241636749,-16.3910189213341,
20.4307288153244));
#157282=CARTESIAN_POINT('Ctrl Pts',(-18.6974043010312,-16.3922615846894,
20.4350449657742));
#157283=CARTESIAN_POINT('Ctrl Pts',(-18.613315412911,-16.3934637745764,
20.4392205394722));
#157284=CARTESIAN_POINT('Ctrl Pts',(-18.5293464168603,-16.3988129730352,
20.4433961131702));
#157285=CARTESIAN_POINT('Ctrl Pts',(-18.4459326746173,-16.4082592081647,
20.4475716868682));
#157286=CARTESIAN_POINT('Ctrl Pts',(-18.3583065652386,-16.4181824751278,
20.4519581256939));
#157287=CARTESIAN_POINT('Ctrl Pts',(-18.2712938422191,-16.432627374356,
20.4563445645197));
#157288=CARTESIAN_POINT('Ctrl Pts',(-18.1853859701635,-16.4514755257613,
20.4607310033455));
#157289=CARTESIAN_POINT('Ctrl Pts',(-18.099478098108,-16.4703236771666,
20.4651174421713));
#157290=CARTESIAN_POINT('Ctrl Pts',(-18.0146756164477,-16.4935748539843,
20.469503880997));
#157291=CARTESIAN_POINT('Ctrl Pts',(-17.9314482086937,-16.5210514974045,
20.4738903198228));
#157292=CARTESIAN_POINT('Ctrl Pts',(-17.8520491312121,-16.5472642583054,
20.4780749893396));
#157293=CARTESIAN_POINT('Ctrl Pts',(-17.7737878973577,-16.5774198558355,
20.4822596588565));
#157294=CARTESIAN_POINT('Ctrl Pts',(-17.6970842217394,-16.6114005748967,
20.4864443283734));
#157295=CARTESIAN_POINT('Ctrl Pts',(-17.6204897187464,-16.6453329290746,
20.4906230418346));
#157296=CARTESIAN_POINT('Ctrl Pts',(-17.545448787571,-16.6830794059288,
20.4948017552959));
#157297=CARTESIAN_POINT('Ctrl Pts',(-17.4723650615669,-16.7244728324609,
20.4989804687571));
#157298=CARTESIAN_POINT('Ctrl Pts',(-17.3979721462502,-16.7666077623972,
20.5032340378299));
#157299=CARTESIAN_POINT('Ctrl Pts',(-17.3256077070819,-16.8125214402581,
20.5074876069027));
#157300=CARTESIAN_POINT('Ctrl Pts',(-17.2556752218673,-16.8619866387128,
20.5117411759755));
#157301=CARTESIAN_POINT('Ctrl Pts',(-17.1870977846746,-16.9104933738853,
20.5159123256928));
#157302=CARTESIAN_POINT('Ctrl Pts',(-17.1208592892441,-16.9624149470776,
20.5200834754102));
#157303=CARTESIAN_POINT('Ctrl Pts',(-17.0573129609309,-17.0174921625856,
20.5242546251275));
#157304=CARTESIAN_POINT('Ctrl Pts',(-16.9937879551552,-17.0725508973092,
20.5284243752439));
#157305=CARTESIAN_POINT('Ctrl Pts',(-16.9329536697872,-17.130762870401,
20.5325941253604));
#157306=CARTESIAN_POINT('Ctrl Pts',(-16.8751302869621,-17.1918285907473,
20.5367638754768));
#157307=CARTESIAN_POINT('Ctrl Pts',(-16.8173089615946,-17.252892138268,
20.5409334772262));
#157308=CARTESIAN_POINT('Ctrl Pts',(-16.76249864144,-17.3168088965337,20.5451030789756));
#157309=CARTESIAN_POINT('Ctrl Pts',(-16.7109817002441,-17.383243499184,
20.549272680725));
#157310=CARTESIAN_POINT('Ctrl Pts',(-16.6576544669953,-17.4520125966707,
20.5535888012066));
#157311=CARTESIAN_POINT('Ctrl Pts',(-16.6078567053803,-17.5234793715945,
20.5579049216882));
#157312=CARTESIAN_POINT('Ctrl Pts',(-16.561853993216,-17.5972373915654,
20.5622210421698));
#157313=CARTESIAN_POINT('Ctrl Pts',(-16.5173490008796,-17.6685940564038,
20.566396641823));
#157314=CARTESIAN_POINT('Ctrl Pts',(-16.4763959254939,-17.7420946281061,
20.5705722414761));
#157315=CARTESIAN_POINT('Ctrl Pts',(-16.439188403649,-17.8173459834589,
20.5747478411293));
#157316=CARTESIAN_POINT('Ctrl Pts',(-16.4001026730812,-17.8963959726636,
20.5791342220251));
#157317=CARTESIAN_POINT('Ctrl Pts',(-16.3651508237527,-17.9773776173555,
20.5835206029209));
#157318=CARTESIAN_POINT('Ctrl Pts',(-16.3344993304474,-18.0598136199109,
20.5879069838167));
#157319=CARTESIAN_POINT('Ctrl Pts',(-16.303847837142,-18.1422496224663,
20.5922933647126));
#157320=CARTESIAN_POINT('Ctrl Pts',(-16.2774968011627,-18.2261394066298,
20.5966797456084));
#157321=CARTESIAN_POINT('Ctrl Pts',(-16.2555511525118,-18.3109919576289,
20.6010661265042));
#157322=CARTESIAN_POINT('Ctrl Pts',(-16.2346154345157,-18.3919396255348,
20.6052506477694));
#157323=CARTESIAN_POINT('Ctrl Pts',(-16.2176106157921,-18.4740647181833,
20.6094351690347));
#157324=CARTESIAN_POINT('Ctrl Pts',(-16.2046649096203,-18.5569506352697,
20.6136196902999));
#157325=CARTESIAN_POINT('Ctrl Pts',(-16.1917376309692,-18.6397185686836,
20.6177982551227));
#157326=CARTESIAN_POINT('Ctrl Pts',(-16.1828580584881,-18.7232447247141,
20.6219768199456));
#157327=CARTESIAN_POINT('Ctrl Pts',(-16.1781041153419,-18.8070992519427,
20.6261553847685));
#157328=CARTESIAN_POINT('Ctrl Pts',(-16.1732647978195,-18.8924596928357,
20.6304089909525));
#157329=CARTESIAN_POINT('Ctrl Pts',(-16.1727008779273,-18.9781599489879,
20.6346625971366));
#157330=CARTESIAN_POINT('Ctrl Pts',(-16.1764397017154,-19.0637377314902,
20.6389162033206));
#157331=CARTESIAN_POINT('Ctrl Pts',(-16.1801059175876,-19.1476535944187,
20.6430872045204));
#157332=CARTESIAN_POINT('Ctrl Pts',(-16.1879092316882,-19.2314512172152,
20.6472582057202));
#157333=CARTESIAN_POINT('Ctrl Pts',(-16.1998229036826,-19.3146933201762,
20.65142920692));
#157334=CARTESIAN_POINT('Ctrl Pts',(-16.2117325790265,-19.3979074981112,
20.6555988088842));
#157335=CARTESIAN_POINT('Ctrl Pts',(-16.2277498086426,-19.480566071281,
20.6597684108483));
#157336=CARTESIAN_POINT('Ctrl Pts',(-16.2477960843791,-19.5622377323235,
20.6639380128125));
#157337=CARTESIAN_POINT('Ctrl Pts',(-16.267841649488,-19.6439064981583,
20.668107466967));
#157338=CARTESIAN_POINT('Ctrl Pts',(-16.2919158662461,-19.7245879748305,
20.6722769211214));
#157339=CARTESIAN_POINT('Ctrl Pts',(-16.3198895960845,-19.8038632271128,
20.6764463752759));
#157340=CARTESIAN_POINT('Ctrl Pts',(-16.3488485215243,-19.8859304427941,
20.6807626717684));
#157341=CARTESIAN_POINT('Ctrl Pts',(-16.3819865838885,-19.9664900366012,
20.6850789682608));
#157342=CARTESIAN_POINT('Ctrl Pts',(-16.419105751819,-20.0450986322096,
20.6893952647533));
#157343=CARTESIAN_POINT('Ctrl Pts',(-16.4550137144481,-20.1211422148331,
20.6935707196945));
#157344=CARTESIAN_POINT('Ctrl Pts',(-16.494646706784,-20.1953597704703,
20.6977461746357));
#157345=CARTESIAN_POINT('Ctrl Pts',(-16.5377789910434,-20.2673757181192,
20.7019216295769));
#157346=CARTESIAN_POINT('Ctrl Pts',(-16.5830936067771,-20.3430354020531,
20.7063083468451));
#157347=CARTESIAN_POINT('Ctrl Pts',(-16.6322706296986,-20.4162643312086,
20.7106950641132));
#157348=CARTESIAN_POINT('Ctrl Pts',(-16.6849987382266,-20.4866640770054,
20.7150817813813));
#157349=CARTESIAN_POINT('Ctrl Pts',(-16.7377268467545,-20.5570638228022,
20.7194684986494));
#157350=CARTESIAN_POINT('Ctrl Pts',(-16.7940056108791,-20.6246339879283,
20.7238552159176));
#157351=CARTESIAN_POINT('Ctrl Pts',(-16.8534788452301,-20.689020491089,
20.7282419331857));
#157352=CARTESIAN_POINT('Ctrl Pts',(-16.9102019255006,-20.7504296413894,
20.7324258004066));
#157353=CARTESIAN_POINT('Ctrl Pts',(-16.9700416973334,-20.8091716375129,
20.7366096676276));
#157354=CARTESIAN_POINT('Ctrl Pts',(-17.0327174072577,-20.8649133643822,
20.7407935348485));
#157355=CARTESIAN_POINT('Ctrl Pts',(-17.0784953144305,-20.9056267380537,
20.7438494026718));
#157356=CARTESIAN_POINT('Ctrl Pts',(-17.1257851938307,-20.944740111196,
20.7469052704952));
#157357=CARTESIAN_POINT('Ctrl Pts',(-17.1744641402402,-20.9821349467765,
20.7499611383185));
#157358=CARTESIAN_POINT('Ctrl Pts',(-17.1744641402401,-20.9821349467765,
19.9498236254873));
#157359=CARTESIAN_POINT('Ctrl Pts',(-17.2410374779127,-21.0332761320307,
19.9540083528391));
#157360=CARTESIAN_POINT('Ctrl Pts',(-17.3100350925294,-21.0810671210711,
19.9581930801908));
#157361=CARTESIAN_POINT('Ctrl Pts',(-17.3810772332865,-21.125292430233,
19.9623778075426));
#157362=CARTESIAN_POINT('Ctrl Pts',(-17.396974538177,-21.1351888553144,
19.9633142360608));
#157363=CARTESIAN_POINT('Ctrl Pts',(-17.4129741317038,-21.1449069178138,
19.9642506645789));
#157364=CARTESIAN_POINT('Ctrl Pts',(-17.4290716122084,-21.1544445288669,
19.965187093097));
#157365=CARTESIAN_POINT('Ctrl Pts',(-17.5010067187011,-21.1970654263791,
19.9693717283979));
#157366=CARTESIAN_POINT('Ctrl Pts',(-17.5751659818923,-21.2362376725991,
19.9735563636989));
#157367=CARTESIAN_POINT('Ctrl Pts',(-17.6511848628853,-21.2717222632969,
19.9777409989998));
#157368=CARTESIAN_POINT('Ctrl Pts',(-17.7270955401341,-21.307156345943,
19.9819196779751));
#157369=CARTESIAN_POINT('Ctrl Pts',(-17.8048601642346,-21.3389130061849,
19.9860983569504));
#157370=CARTESIAN_POINT('Ctrl Pts',(-17.8840874846203,-21.3667978623895,
19.9902770359257));
#157371=CARTESIAN_POINT('Ctrl Pts',(-17.9647348763174,-21.3951825270456,
19.9945306135862));
#157372=CARTESIAN_POINT('Ctrl Pts',(-18.0468975021298,-21.4195549745919,
19.9987841912467));
#157373=CARTESIAN_POINT('Ctrl Pts',(-18.1301389338575,-21.4397604010027,
20.0030377689073));
#157374=CARTESIAN_POINT('Ctrl Pts',(-18.211766588852,-21.4595741108567,
20.0072088837303));
#157375=CARTESIAN_POINT('Ctrl Pts',(-18.294431126417,-21.4753808138487,
20.0113799985532));
#157376=CARTESIAN_POINT('Ctrl Pts',(-18.3777050585878,-21.4870845971533,
20.0155511133762));
#157377=CARTESIAN_POINT('Ctrl Pts',(-18.4609510470138,-21.4987844530881,
20.0197208285227));
#157378=CARTESIAN_POINT('Ctrl Pts',(-18.544805568747,-21.5063840596946,
20.0238905436692));
#157379=CARTESIAN_POINT('Ctrl Pts',(-18.6288324774106,-21.5098388909766,
20.0280602588157));
#157380=CARTESIAN_POINT('Ctrl Pts',(-18.7128563956357,-21.5132935993045,
20.0322298255659));
#157381=CARTESIAN_POINT('Ctrl Pts',(-18.7970522289137,-21.5126038075458,
20.0363993923161));
#157382=CARTESIAN_POINT('Ctrl Pts',(-18.8809816357491,-21.5077770635861,
20.0405689590663));
#157383=CARTESIAN_POINT('Ctrl Pts',(-18.9678618598034,-21.5027806194017,
20.0448851207924));
#157384=CARTESIAN_POINT('Ctrl Pts',(-19.0544560474151,-21.4933509339533,
20.0492012825184));
#157385=CARTESIAN_POINT('Ctrl Pts',(-19.1402833032842,-21.4795549207629,
20.0535174442444));
#157386=CARTESIAN_POINT('Ctrl Pts',(-19.2233147796994,-21.466208305725,
20.057693009185));
#157387=CARTESIAN_POINT('Ctrl Pts',(-19.3056280710303,-21.4487756011034,
20.0618685741256));
#157388=CARTESIAN_POINT('Ctrl Pts',(-19.3867996160279,-21.4273691969712,
20.0660441390663));
#157389=CARTESIAN_POINT('Ctrl Pts',(-19.472070890686,-21.4048816199976,
20.070430599185));
#157390=CARTESIAN_POINT('Ctrl Pts',(-19.5560814940463,-21.3780085540522,
20.0748170593037));
#157391=CARTESIAN_POINT('Ctrl Pts',(-19.6383622324208,-21.3469381938937,
20.0792035194224));
#157392=CARTESIAN_POINT('Ctrl Pts',(-19.7206429707954,-21.3158678337352,
20.0835899795411));
#157393=CARTESIAN_POINT('Ctrl Pts',(-19.8011933431874,-21.2806004817501,
20.0879764396598));
#157394=CARTESIAN_POINT('Ctrl Pts',(-19.8795742651246,-21.2413797420009,
20.0923628997785));
#157395=CARTESIAN_POINT('Ctrl Pts',(-19.9543489008138,-21.2039635384947,
20.0965475399847));
#157396=CARTESIAN_POINT('Ctrl Pts',(-20.0274276531195,-21.162810473499,
20.100732180191));
#157397=CARTESIAN_POINT('Ctrl Pts',(-20.0984122388012,-21.11809769923,20.1049168203972));
#157398=CARTESIAN_POINT('Ctrl Pts',(-20.1692957874189,-21.0734485676151,
20.1090955043278));
#157399=CARTESIAN_POINT('Ctrl Pts',(-20.2380907042344,-21.0252500340151,
20.1132741882584));
#157400=CARTESIAN_POINT('Ctrl Pts',(-20.3044217681325,-20.9737258642496,
20.117452872189));
#157401=CARTESIAN_POINT('Ctrl Pts',(-20.371941651073,-20.9212782521244,
20.1217064486169));
#157402=CARTESIAN_POINT('Ctrl Pts',(-20.4369080609029,-20.865384834865,
20.1259600250449));
#157403=CARTESIAN_POINT('Ctrl Pts',(-20.4989546028882,-20.8063287868509,
20.1302136014728));
#157404=CARTESIAN_POINT('Ctrl Pts',(-20.5597983582893,-20.7484175540028,
20.1343847213367));
#157405=CARTESIAN_POINT('Ctrl Pts',(-20.6178340917841,-20.6874655447192,
20.1385558412007));
#157406=CARTESIAN_POINT('Ctrl Pts',(-20.6727497644134,-20.6237802938745,
20.1427269610646));
#157407=CARTESIAN_POINT('Ctrl Pts',(-20.7276470096087,-20.5601164131724,
20.1468966812728));
#157408=CARTESIAN_POINT('Ctrl Pts',(-20.7794259730566,-20.4937214605129,
20.151066401481));
#157409=CARTESIAN_POINT('Ctrl Pts',(-20.827813137392,-20.4249380658006,
20.1552361216892));
#157410=CARTESIAN_POINT('Ctrl Pts',(-20.8761985798384,-20.3561571187907,
20.1594056935151));
#157411=CARTESIAN_POINT('Ctrl Pts',(-20.921192199164,-20.2849882754667,
20.1635752653411));
#157412=CARTESIAN_POINT('Ctrl Pts',(-20.9625630757428,-20.2118041980546,
20.167744837167));
#157413=CARTESIAN_POINT('Ctrl Pts',(-21.0053883717902,-20.1360472878725,
20.1720609929414));
#157414=CARTESIAN_POINT('Ctrl Pts',(-21.044331197893,-20.0581312678785,
20.1763771487158));
#157415=CARTESIAN_POINT('Ctrl Pts',(-21.0791875194638,-19.9784967114177,
20.1806933044902));
#157416=CARTESIAN_POINT('Ctrl Pts',(-21.1129085013345,-19.9014560108021,
20.184868874489));
#157417=CARTESIAN_POINT('Ctrl Pts',(-21.1428049796707,-19.8228074643854,
20.1890444444878));
#157418=CARTESIAN_POINT('Ctrl Pts',(-21.1687421906793,-19.7429680555664,
20.1932200144866));
#157419=CARTESIAN_POINT('Ctrl Pts',(-21.1959893077345,-19.6590965199184,
20.1976064631488));
#157420=CARTESIAN_POINT('Ctrl Pts',(-21.2188665683597,-19.5739112349382,
20.201992911811));
#157421=CARTESIAN_POINT('Ctrl Pts',(-21.2372782494394,-19.4879085797817,
20.2063793604732));
#157422=CARTESIAN_POINT('Ctrl Pts',(-21.2556899305191,-19.4019059246253,
20.2107658091355));
#157423=CARTESIAN_POINT('Ctrl Pts',(-21.2696360151318,-19.3150864842148,
20.2151522577977));
#157424=CARTESIAN_POINT('Ctrl Pts',(-21.2790836671994,-19.2279513126528,
20.2195387064599));
#157425=CARTESIAN_POINT('Ctrl Pts',(-21.2889563823072,-19.136895808223,
20.2241225075637));
#157426=CARTESIAN_POINT('Ctrl Pts',(-21.2939437779019,-19.0453011468624,
20.2287063086676));
#157427=CARTESIAN_POINT('Ctrl Pts',(-21.2939995273701,-18.9535555915677,
20.2332901097715));
#157428=CARTESIAN_POINT('',(-21.2937660523048,-18.9509923322678,20.1667099325986));
#157429=CARTESIAN_POINT('Ctrl Pts',(-17.1744641402401,-20.9821349467765,
19.8833624839903));
#157430=CARTESIAN_POINT('Ctrl Pts',(-17.2411053585891,-21.0333282775047,
19.8875327609786));
#157431=CARTESIAN_POINT('Ctrl Pts',(-17.3103076802409,-21.0812658121085,
19.8917030379669));
#157432=CARTESIAN_POINT('Ctrl Pts',(-17.3817163438391,-21.1256901603679,
19.8958733149552));
#157433=CARTESIAN_POINT('Ctrl Pts',(-17.4531114624803,-21.1701060821163,
19.9000428009159));
#157434=CARTESIAN_POINT('Ctrl Pts',(-17.5267117010556,-21.211009898609,
19.9042122868766));
#157435=CARTESIAN_POINT('Ctrl Pts',(-17.6021341277255,-21.2481880687741,
19.9083817728373));
#157436=CARTESIAN_POINT('Ctrl Pts',(-17.6775648727756,-21.2853703393396,
19.9125517186529));
#157437=CARTESIAN_POINT('Ctrl Pts',(-17.754817791772,-21.3188259454625,
19.9167216644685));
#157438=CARTESIAN_POINT('Ctrl Pts',(-17.833487460302,-21.3483883587279,
19.920891610284));
#157439=CARTESIAN_POINT('Ctrl Pts',(-17.9122410721742,-21.3779823161427,
19.9250660055805));
#157440=CARTESIAN_POINT('Ctrl Pts',(-17.9924140202009,-21.4036746249937,
19.929240400877));
#157441=CARTESIAN_POINT('Ctrl Pts',(-18.0735835869046,-21.4253479660804,
19.9334147961735));
#157442=CARTESIAN_POINT('Ctrl Pts',(-18.1547995551522,-21.4470336969892,
19.9375915778125));
#157443=CARTESIAN_POINT('Ctrl Pts',(-18.2370128265568,-21.464695789383,
19.9417683594515));
#157444=CARTESIAN_POINT('Ctrl Pts',(-18.3197906755089,-21.4782681242308,
19.9459451410904));
#157445=CARTESIAN_POINT('Ctrl Pts',(-18.4027095772105,-21.4918635862215,
19.9501290399297));
#157446=CARTESIAN_POINT('Ctrl Pts',(-18.4861945203917,-21.5013553226401,
19.9543129387691));
#157447=CARTESIAN_POINT('Ctrl Pts',(-18.5698081482532,-21.5067291511665,
19.9584968376084));
#157448=CARTESIAN_POINT('Ctrl Pts',(-18.6237986730703,-21.5101991097108,
19.9611984414006));
#157449=CARTESIAN_POINT('Ctrl Pts',(-18.6778428224662,-21.5119531844675,
19.9639000451929));
#157450=CARTESIAN_POINT('Ctrl Pts',(-18.7318236815561,-21.5119990749291,
19.9666016489852));
#157451=CARTESIAN_POINT('Ctrl Pts',(-18.8154370559313,-21.5120701567239,
19.9707862843005));
#157452=CARTESIAN_POINT('Ctrl Pts',(-18.8992095169516,-21.508040657495,
19.9749709196158));
#157453=CARTESIAN_POINT('Ctrl Pts',(-18.9827056283928,-21.4998904039236,
19.9791555549311));
#157454=CARTESIAN_POINT('Ctrl Pts',(-19.0660828935662,-21.4917517512183,
19.9833342339415));
#157455=CARTESIAN_POINT('Ctrl Pts',(-19.149184136535,-21.4795040389676,
19.987512912952));
#157456=CARTESIAN_POINT('Ctrl Pts',(-19.2315736418543,-21.4631790997322,
19.9916915919625));
#157457=CARTESIAN_POINT('Ctrl Pts',(-19.3154398966918,-21.446561552281,
19.9959451696169));
#157458=CARTESIAN_POINT('Ctrl Pts',(-19.3985681653821,-21.4257191734759,
20.0001987472712));
#157459=CARTESIAN_POINT('Ctrl Pts',(-19.4805039905309,-21.400740858507,
20.0044523249255));
#157460=CARTESIAN_POINT('Ctrl Pts',(-19.560851352111,-21.3762467901208,
20.0086234398338));
#157461=CARTESIAN_POINT('Ctrl Pts',(-19.6400516322992,-21.3477758589918,
20.0127945547421));
#157462=CARTESIAN_POINT('Ctrl Pts',(-19.7176880451009,-21.315463101029,
20.0169656696504));
#157463=CARTESIAN_POINT('Ctrl Pts',(-19.7952984062491,-21.2831611859264,
20.0211353849005));
#157464=CARTESIAN_POINT('Ctrl Pts',(-19.8713455178527,-21.247020180909,
20.0253051001507));
#157465=CARTESIAN_POINT('Ctrl Pts',(-19.9454312973038,-21.207223760941,
20.0294748154008));
#157466=CARTESIAN_POINT('Ctrl Pts',(-20.0195144404333,-21.1674287571174,
20.0336443822728));
#157467=CARTESIAN_POINT('Ctrl Pts',(-20.0916359853166,-21.1239788154148,
20.0378139491447));
#157468=CARTESIAN_POINT('Ctrl Pts',(-20.1614224658083,-21.0771035513842,
20.0419835160167));
#157469=CARTESIAN_POINT('Ctrl Pts',(-20.2336625183512,-21.0285802340787,
20.0462996776542));
#157470=CARTESIAN_POINT('Ctrl Pts',(-20.3033998142158,-20.9763865417844,
20.0506158392917));
#157471=CARTESIAN_POINT('Ctrl Pts',(-20.3702544760718,-20.9208248498876,
20.0549320009292));
#157472=CARTESIAN_POINT('Ctrl Pts',(-20.4349313850112,-20.8670730487781,
20.0591075660348));
#157473=CARTESIAN_POINT('Ctrl Pts',(-20.4969102618753,-20.8101696539257,
20.0632831311405));
#157474=CARTESIAN_POINT('Ctrl Pts',(-20.555883728143,-20.7504270018902,
20.0674586962461));
#157475=CARTESIAN_POINT('Ctrl Pts',(-20.6178357606473,-20.6876669344389,
20.0718451561495));
#157476=CARTESIAN_POINT('Ctrl Pts',(-20.6764704135552,-20.6217736908107,
20.0762316160529));
#157477=CARTESIAN_POINT('Ctrl Pts',(-20.7314796147868,-20.5531480845041,
20.0806180759564));
#157478=CARTESIAN_POINT('Ctrl Pts',(-20.7864888160183,-20.4845224781975,
20.0850045358598));
#157479=CARTESIAN_POINT('Ctrl Pts',(-20.8378722882511,-20.4131650245059,
20.0893909957632));
#157480=CARTESIAN_POINT('Ctrl Pts',(-20.8853760799667,-20.3395089053938,
20.0937774556666));
#157481=CARTESIAN_POINT('Ctrl Pts',(-20.93172083375,-20.2676499109516,20.0980568909888));
#157482=CARTESIAN_POINT('Ctrl Pts',(-20.9745398784111,-20.1933453659579,
20.1023363263109));
#157483=CARTESIAN_POINT('Ctrl Pts',(-21.0135728621542,-20.1169667661055,
20.1066157616331));
#157484=CARTESIAN_POINT('Ctrl Pts',(-21.0525424988234,-20.0407121219527,
20.1108882518109));
#157485=CARTESIAN_POINT('Ctrl Pts',(-21.0877380945303,-19.9623904961899,
20.1151607419887));
#157486=CARTESIAN_POINT('Ctrl Pts',(-21.1189429603293,-19.8824015670536,
20.1194332321666));
#157487=CARTESIAN_POINT('Ctrl Pts',(-21.1500944336146,-19.8025495015083,
20.1236984119784));
#157488=CARTESIAN_POINT('Ctrl Pts',(-21.1772686126578,-19.7210362114978,
20.1279635917902));
#157489=CARTESIAN_POINT('Ctrl Pts',(-21.2002957121622,-19.6382838043918,
20.132228771602));
#157490=CARTESIAN_POINT('Ctrl Pts',(-21.2232995983466,-19.5556148189128,
20.1364896517415));
#157491=CARTESIAN_POINT('Ctrl Pts',(-21.242164599727,-19.4717096138904,
20.1407505318809));
#157492=CARTESIAN_POINT('Ctrl Pts',(-21.2567699769455,-19.3870076360505,
20.1450114120204));
#157493=CARTESIAN_POINT('Ctrl Pts',(-21.2713627640963,-19.3023786726647,
20.1492686192133));
#157494=CARTESIAN_POINT('Ctrl Pts',(-21.2817031592285,-19.2169547278876,
20.1535258264062));
#157495=CARTESIAN_POINT('Ctrl Pts',(-21.2877212407691,-19.1311865632376,
20.1577830335991));
#157496=CARTESIAN_POINT('Ctrl Pts',(-21.2919276409326,-19.0712380199392,
20.1607586524755));
#157497=CARTESIAN_POINT('Ctrl Pts',(-21.2940234518483,-19.0111215769093,
20.163734271352));
#157498=CARTESIAN_POINT('Ctrl Pts',(-21.293999801981,-18.9509930952203,
20.1667098902285));
#157499=CARTESIAN_POINT('Ctrl Pts',(-21.2901593135592,-18.9509805599729,
20.1667105863666));
#157500=CARTESIAN_POINT('Ctrl Pts',(-21.2914430747328,-18.5861666271369,
20.1847914783605));
#157501=CARTESIAN_POINT('Ctrl Pts',(-21.0477247281039,-17.3676608534593,
20.2452643059147));
#157502=CARTESIAN_POINT('Ctrl Pts',(-19.1741877080397,-15.9570837783716,
20.3481290690295));
#157503=CARTESIAN_POINT('Ctrl Pts',(-16.4540143744161,-16.9607794391954,
20.4753048757109));
#157504=CARTESIAN_POINT('Ctrl Pts',(-15.9020682314716,-19.4468144996336,
20.5870029204769));
#157505=CARTESIAN_POINT('Ctrl Pts',(-16.7482596976323,-20.6463211842255,
20.6563090296824));
#157506=CARTESIAN_POINT('Ctrl Pts',(-17.1763037530771,-20.9797762769264,
20.6832232033273));
#157507=CARTESIAN_POINT('Origin',(-18.734,-18.952,-1.76670989022851));
#157508=CARTESIAN_POINT('',(-17.176996236551,-20.9788220778502,21.5499224931685));
#157509=CARTESIAN_POINT('',(-17.1722616776481,-20.9849677398537,21.4832513321535));
#157510=CARTESIAN_POINT('',(-17.1744641402401,-20.9821349467765,-1.76670989022851));
#157511=CARTESIAN_POINT('',(-21.293894749231,-18.9533416782113,21.033290082045));
#157512=CARTESIAN_POINT('Ctrl Pts',(-21.2904839170199,-18.9533393312605,
21.0332901097715));
#157513=CARTESIAN_POINT('Ctrl Pts',(-21.2880301337774,-18.4391275099938,
21.0587831909243));
#157514=CARTESIAN_POINT('Ctrl Pts',(-20.8878308621683,-17.0663417376224,
21.1266682076376));
#157515=CARTESIAN_POINT('Ctrl Pts',(-18.6471935206347,-15.9262791991665,
21.2369451599114));
#157516=CARTESIAN_POINT('Ctrl Pts',(-16.142559944897,-17.3869838835127,
21.3641209665928));
#157517=CARTESIAN_POINT('Ctrl Pts',(-16.0386998683022,-19.7637662988606,
21.4684467443452));
#157518=CARTESIAN_POINT('Ctrl Pts',(-16.8637710355043,-20.7393377348947,
21.5303805865371));
#157519=CARTESIAN_POINT('Ctrl Pts',(-17.176996236551,-20.9788220778502,
21.5499224931685));
#157520=CARTESIAN_POINT('Ctrl Pts',(-17.1744641402402,-20.9821349467765,
20.7499611383185));
#157521=CARTESIAN_POINT('Ctrl Pts',(-17.2444594813357,-21.0359048917883,
20.754355163383));
#157522=CARTESIAN_POINT('Ctrl Pts',(-17.317328415444,-21.0861194210246,
20.7587491884476));
#157523=CARTESIAN_POINT('Ctrl Pts',(-17.3926684715169,-21.1324654848672,
20.7631432135121));
#157524=CARTESIAN_POINT('Ctrl Pts',(-17.4641970336474,-21.1764668764227,
20.7673149424862));
#157525=CARTESIAN_POINT('Ctrl Pts',(-17.5379523384401,-21.2169813963177,
20.7714866714603));
#157526=CARTESIAN_POINT('Ctrl Pts',(-17.6135584513473,-21.2537842505441,
20.7756584004345));
#157527=CARTESIAN_POINT('Ctrl Pts',(-17.6891338306681,-21.2905721445555,
20.7798284336172));
#157528=CARTESIAN_POINT('Ctrl Pts',(-17.7665581109874,-21.3236511679191,
20.7839984668));
#157529=CARTESIAN_POINT('Ctrl Pts',(-17.8454309959992,-21.3528425864952,
20.7881684999828));
#157530=CARTESIAN_POINT('Ctrl Pts',(-17.9242954765414,-21.382030894517,
20.7923380888187));
#157531=CARTESIAN_POINT('Ctrl Pts',(-18.0046078235079,-21.4073322617217,
20.7965076776546));
#157532=CARTESIAN_POINT('Ctrl Pts',(-18.0859492963724,-21.4286167013746,
20.8006772664906));
#157533=CARTESIAN_POINT('Ctrl Pts',(-18.1673064987639,-21.4499052569374,
20.8048476616269));
#157534=CARTESIAN_POINT('Ctrl Pts',(-18.2496927769265,-21.4671752273624,
20.8090180567632));
#157535=CARTESIAN_POINT('Ctrl Pts',(-18.3326771588405,-21.4803472817561,
20.8131884518995));
#157536=CARTESIAN_POINT('Ctrl Pts',(-18.4157540106533,-21.4935340138339,
20.8173634941273));
#157537=CARTESIAN_POINT('Ctrl Pts',(-18.4994298412268,-21.502613645428,
20.8215385363551));
#157538=CARTESIAN_POINT('Ctrl Pts',(-18.583267037094,-21.5075585639726,
20.825713578583));
#157539=CARTESIAN_POINT('Ctrl Pts',(-18.6671584017786,-21.5125066775237,
20.8298913183855));
#157540=CARTESIAN_POINT('Ctrl Pts',(-18.7512108797419,-21.5133147567839,
20.834069058188));
#157541=CARTESIAN_POINT('Ctrl Pts',(-18.8349877178507,-21.5100073261903,
20.8382467979905));
#157542=CARTESIAN_POINT('Ctrl Pts',(-18.9189003229372,-21.5066945356444,
20.8424313081501));
#157543=CARTESIAN_POINT('Ctrl Pts',(-19.0025359395193,-21.4992529664416,
20.8466158183097));
#157544=CARTESIAN_POINT('Ctrl Pts',(-19.0854642865313,-21.487758832242,
20.8508003284693));
#157545=CARTESIAN_POINT('Ctrl Pts',(-19.1159668049541,-21.4835310856051,
20.8523394656019));
#157546=CARTESIAN_POINT('Ctrl Pts',(-19.1463737547783,-21.478755563272,
20.8538786027345));
#157547=CARTESIAN_POINT('Ctrl Pts',(-19.1766642018011,-21.4734377653323,
20.8554177398671));
#157548=CARTESIAN_POINT('Ctrl Pts',(-19.2590223589629,-21.4589789480642,
20.8596025740416));
#157549=CARTESIAN_POINT('Ctrl Pts',(-19.3408245084339,-21.4404538839632,
20.8637874082161));
#157550=CARTESIAN_POINT('Ctrl Pts',(-19.4216382989709,-21.4179184029056,
20.8679722423906));
#157551=CARTESIAN_POINT('Ctrl Pts',(-19.5023371028523,-21.3954149866674,
20.8721511221348));
#157552=CARTESIAN_POINT('Ctrl Pts',(-19.5820499018622,-21.3689126104334,
20.8763300018789));
#157553=CARTESIAN_POINT('Ctrl Pts',(-19.6603531104248,-21.338518366744,
20.8805088816231));
#157554=CARTESIAN_POINT('Ctrl Pts',(-19.7400550610479,-21.3075811860814,
20.8847624093283));
#157555=CARTESIAN_POINT('Ctrl Pts',(-19.8182960912148,-21.2726118104529,
20.8890159370335));
#157556=CARTESIAN_POINT('Ctrl Pts',(-19.8946441530214,-21.2337767528961,
20.8932694647388));
#157557=CARTESIAN_POINT('Ctrl Pts',(-19.9695166174632,-21.195692269843,
20.8974407834904));
#157558=CARTESIAN_POINT('Ctrl Pts',(-20.0425682056166,-21.1538904198174,
20.901612102242));
#157559=CARTESIAN_POINT('Ctrl Pts',(-20.1134119104384,-21.1085766347016,
20.9057834209936));
#157560=CARTESIAN_POINT('Ctrl Pts',(-20.1842318561761,-21.0632780466174,
20.9099533407964));
#157561=CARTESIAN_POINT('Ctrl Pts',(-20.2528450019901,-21.0144701102459,
20.9141232605992));
#157562=CARTESIAN_POINT('Ctrl Pts',(-20.3188912127324,-20.9624029058384,
20.9182931804021));
#157563=CARTESIAN_POINT('Ctrl Pts',(-20.3849350802549,-20.9103375486967,
20.9224629522624));
#157564=CARTESIAN_POINT('Ctrl Pts',(-20.448411833077,-20.8550134388734,
20.9266327241228));
#157565=CARTESIAN_POINT('Ctrl Pts',(-20.5089935615136,-20.7967216203496,
20.9308024959832));
#157566=CARTESIAN_POINT('Ctrl Pts',(-20.5716986579763,-20.7363866943274,
20.9351184168636));
#157567=CARTESIAN_POINT('Ctrl Pts',(-20.6313016391124,-20.6728725241964,
20.9394343377441));
#157568=CARTESIAN_POINT('Ctrl Pts',(-20.687481020985,-20.6065428071378,
20.9437502586245));
#157569=CARTESIAN_POINT('Ctrl Pts',(-20.7418360778663,-20.5423670290593,
20.9479260276902));
#157570=CARTESIAN_POINT('Ctrl Pts',(-20.79298623453,-20.4755561680757,20.9521017967558));
#157571=CARTESIAN_POINT('Ctrl Pts',(-20.8406830326348,-20.4064712441326,
20.9562775658215));
#157572=CARTESIAN_POINT('Ctrl Pts',(-20.8907811103752,-20.333908262383,
20.9606635626093));
#157573=CARTESIAN_POINT('Ctrl Pts',(-20.9370686806316,-20.2588367305564,
20.9650495593971));
#157574=CARTESIAN_POINT('Ctrl Pts',(-20.9793120741947,-20.1817047163753,
20.969435556185));
#157575=CARTESIAN_POINT('Ctrl Pts',(-21.0215554677577,-20.1045727021941,
20.9738215529728));
#157576=CARTESIAN_POINT('Ctrl Pts',(-21.0597545011784,-20.025380760798,
20.9782075497606));
#157577=CARTESIAN_POINT('Ctrl Pts',(-21.0937343889893,-19.9445994224366,
20.9825935465485));
#157578=CARTESIAN_POINT('Ctrl Pts',(-21.1297844964522,-19.8588964929525,
20.9872467595436));
#157579=CARTESIAN_POINT('Ctrl Pts',(-21.1612011352353,-19.7711341998165,
20.9918999725387));
#157580=CARTESIAN_POINT('Ctrl Pts',(-21.187770405969,-19.6818018873577,
20.9965531855338));
#157581=CARTESIAN_POINT('Ctrl Pts',(-21.2142564631891,-19.5927493588517,
21.0011918249184));
#157582=CARTESIAN_POINT('Ctrl Pts',(-21.2359253189815,-19.5021368713044,
21.005830464303));
#157583=CARTESIAN_POINT('Ctrl Pts',(-21.2526114126831,-19.410471975046,
21.0104691036876));
#157584=CARTESIAN_POINT('Ctrl Pts',(-21.269207206213,-19.3193031419175,
21.0150826401368));
#157585=CARTESIAN_POINT('Ctrl Pts',(-21.2808739033347,-19.2270935185721,
21.019696176586));
#157586=CARTESIAN_POINT('Ctrl Pts',(-21.2874964963647,-19.1343612981233,
21.0243097130352));
#157587=CARTESIAN_POINT('Ctrl Pts',(-21.2917935126354,-19.074192742048,
21.0273031690875));
#157588=CARTESIAN_POINT('Ctrl Pts',(-21.2939679585382,-19.0138045492422,
21.0302966251399));
#157589=CARTESIAN_POINT('Ctrl Pts',(-21.29399964838,-18.9533417503911,21.0332900811922));
#157590=CARTESIAN_POINT('',(-21.2964370555865,-18.950145562236,20.9667098902285));
#157591=CARTESIAN_POINT('Ctrl Pts',(-17.1763037530771,-20.9797762769264,
20.6832232033273));
#157592=CARTESIAN_POINT('Ctrl Pts',(-17.4224626753946,-21.171539122868,
20.6987009652428));
#157593=CARTESIAN_POINT('Ctrl Pts',(-18.4657781128202,-21.7248573720238,
20.7565706627188));
#157594=CARTESIAN_POINT('Ctrl Pts',(-20.5735369035609,-21.279131873543,
20.8510662250192));
#157595=CARTESIAN_POINT('Ctrl Pts',(-21.2904547875037,-19.6845342581055,
20.9300840254041));
#157596=CARTESIAN_POINT('Ctrl Pts',(-21.2964370555865,-18.950145562236,
20.9667098902285));
#157597=CARTESIAN_POINT('Ctrl Pts',(-21.2964370555865,-18.950145562236,
20.9667098902285));
#157598=CARTESIAN_POINT('Ctrl Pts',(-21.2973788539875,-18.8345295300019,
20.9724759609645));
#157599=CARTESIAN_POINT('Ctrl Pts',(-21.2376962631739,-17.8698878407826,
21.0206339672611));
#157600=CARTESIAN_POINT('Ctrl Pts',(-20.0126665202556,-16.2082458119612,
21.1111839091181));
#157601=CARTESIAN_POINT('Ctrl Pts',(-17.1190397035347,-16.3916499423084,
21.2383597157995));
#157602=CARTESIAN_POINT('Ctrl Pts',(-15.7420434390129,-18.8613631757064,
21.3623821901447));
#157603=CARTESIAN_POINT('Ctrl Pts',(-16.5519397204913,-20.5025265151668,
21.4440127289293));
#157604=CARTESIAN_POINT('Ctrl Pts',(-17.1722616776481,-20.9849677398537,
21.4832513321535));
#157605=CARTESIAN_POINT('Origin',(23.734,10.1295,7.));
#157606=CARTESIAN_POINT('',(18.1138504785695,10.1294996219627,11.263));
#157607=CARTESIAN_POINT('',(17.7339525131034,10.1295,11.263));
#157608=CARTESIAN_POINT('',(23.734,10.1295,11.263));
#157609=CARTESIAN_POINT('',(17.733926103998,5.86728159109872,6.91639119716989));
#157610=CARTESIAN_POINT('Ctrl Pts',(17.7339050262067,5.86731958600617,6.91641101407837));
#157611=CARTESIAN_POINT('Ctrl Pts',(17.7472715260208,5.8626834471393,7.15280651591456));
#157612=CARTESIAN_POINT('Ctrl Pts',(17.7606427200251,5.87772229287975,7.38918410650487));
#157613=CARTESIAN_POINT('Ctrl Pts',(17.786815786871,5.94601267161834,7.851385147275));
#157614=CARTESIAN_POINT('Ctrl Pts',(17.7995827838462,5.99822391915381,8.07656087620677));
#157615=CARTESIAN_POINT('Ctrl Pts',(17.835119220085,6.19309530208892,8.6870119457575));
#157616=CARTESIAN_POINT('Ctrl Pts',(17.8583297454841,6.37348892203968,9.05758417879396));
#157617=CARTESIAN_POINT('Ctrl Pts',(17.8967844976297,6.75793497537115,9.62310813562425));
#157618=CARTESIAN_POINT('Ctrl Pts',(17.9119480496723,6.93333891295104,9.83420296144228));
#157619=CARTESIAN_POINT('Ctrl Pts',(17.9585777026362,7.53054826773672,10.4264221396266));
#157620=CARTESIAN_POINT('Ctrl Pts',(17.9907447985597,8.0090078993714,10.7414473723924));
#157621=CARTESIAN_POINT('Ctrl Pts',(18.0356178403253,8.75695927515788,11.0430860995625));
#157622=CARTESIAN_POINT('Ctrl Pts',(18.0487834108318,8.98598833752505,11.1137320441811));
#157623=CARTESIAN_POINT('Ctrl Pts',(18.079255259419,9.51889849517406,11.230142863414));
#157624=CARTESIAN_POINT('Ctrl Pts',(18.0966641306137,9.82391712323077,11.2629999729013));
#157625=CARTESIAN_POINT('Ctrl Pts',(18.1138504785695,10.1294996219628,11.263));
#157626=CARTESIAN_POINT('Origin',(17.734,10.1295,7.));
#157627=CARTESIAN_POINT('Origin',(23.734,10.1295,7.));
#157628=CARTESIAN_POINT('',(19.613681670589,10.1293184243372,11.262999996133));
#157629=CARTESIAN_POINT('',(19.2041804397712,10.1295003962013,11.263));
#157630=CARTESIAN_POINT('',(23.734,10.1295,11.263));
#157631=CARTESIAN_POINT('Ctrl Pts',(18.1138504785695,10.1294996219628,11.263));
#157632=CARTESIAN_POINT('Ctrl Pts',(18.1201665818489,10.2418033311226,11.2630000099589));
#157633=CARTESIAN_POINT('Ctrl Pts',(18.1264604938674,10.3541827562155,11.2585622688176));
#157634=CARTESIAN_POINT('Ctrl Pts',(18.1471940248053,10.7247867279603,11.2291842636932));
#157635=CARTESIAN_POINT('Ctrl Pts',(18.1614507417818,10.9807896977882,11.185172584425));
#157636=CARTESIAN_POINT('Ctrl Pts',(18.1906782807484,11.4871350383031,11.0497141872492));
#157637=CARTESIAN_POINT('Ctrl Pts',(18.2057216972168,11.736119762744,10.957539975328));
#157638=CARTESIAN_POINT('Ctrl Pts',(18.2521519575592,12.4777159151984,10.6014088470678));
#157639=CARTESIAN_POINT('Ctrl Pts',(18.2823429382786,12.9282578663991,10.263620068643));
#157640=CARTESIAN_POINT('Ctrl Pts',(18.3296538137456,13.4877135786547,9.64077045992482));
#157641=CARTESIAN_POINT('Ctrl Pts',(18.3454517805426,13.6535680656264,9.41499876952407));
#157642=CARTESIAN_POINT('Ctrl Pts',(18.3746150682435,13.9198075223705,8.96609205758119));
#157643=CARTESIAN_POINT('Ctrl Pts',(18.3879846661531,14.0254683231313,8.74739252579659));
#157644=CARTESIAN_POINT('Ctrl Pts',(18.4231226715518,14.2511090924869,8.15655366404959));
#157645=CARTESIAN_POINT('Ctrl Pts',(18.4453003814799,14.3395929517634,7.77484194259151));
#157646=CARTESIAN_POINT('Ctrl Pts',(18.4823917739119,14.3994905024371,7.11683170769568));
#157647=CARTESIAN_POINT('Ctrl Pts',(18.4973546022919,14.3982932618793,6.8454803979011));
#157648=CARTESIAN_POINT('Ctrl Pts',(18.5347942990784,14.331175004687,6.17388033575934));
#157649=CARTESIAN_POINT('Ctrl Pts',(18.5577058604119,14.2339831082639,5.77944841219729));
#157650=CARTESIAN_POINT('Ctrl Pts',(18.6118397199921,13.8735896061126,4.88640953402182));
#157651=CARTESIAN_POINT('Ctrl Pts',(18.6422259846235,13.564577504846,4.41432857678637));
#157652=CARTESIAN_POINT('Ctrl Pts',(18.7055321258339,12.7810679852525,3.61529247979986));
#157653=CARTESIAN_POINT('Ctrl Pts',(18.7359957101013,12.313775454571,3.29648891512936));
#157654=CARTESIAN_POINT('Ctrl Pts',(18.7812347552267,11.5729279137528,2.98133967923363));
#157655=CARTESIAN_POINT('Ctrl Pts',(18.7951387469876,11.3397888762334,2.90508645340095));
#157656=CARTESIAN_POINT('Ctrl Pts',(18.8352464587369,10.6462678184755,2.74269823580172));
#157657=CARTESIAN_POINT('Ctrl Pts',(18.8606341833889,10.1767051841473,2.71170941449449));
#157658=CARTESIAN_POINT('Ctrl Pts',(18.9034984090833,9.41910717160332,2.78634983706026));
#157659=CARTESIAN_POINT('Ctrl Pts',(18.9201726621107,9.1304431930615,2.84531616915589));
#157660=CARTESIAN_POINT('Ctrl Pts',(18.9522997376604,8.58351430917128,3.01738452781976));
#157661=CARTESIAN_POINT('Ctrl Pts',(18.9677031918578,8.32577932626899,3.12728891895167));
#157662=CARTESIAN_POINT('Ctrl Pts',(19.0109367485974,7.64338159504519,3.50128156788361));
#157663=CARTESIAN_POINT('Ctrl Pts',(19.0393158831965,7.25153182153395,3.81580315655779));
#157664=CARTESIAN_POINT('Ctrl Pts',(19.0795493216095,6.77548652527038,4.3591967363062));
#157665=CARTESIAN_POINT('Ctrl Pts',(19.0918810594698,6.64150701319289,4.53887176488872));
#157666=CARTESIAN_POINT('Ctrl Pts',(19.1230560174742,6.34314182400765,5.01263327675107));
#157667=CARTESIAN_POINT('Ctrl Pts',(19.1421738225493,6.19829725781291,5.31721393769373));
#157668=CARTESIAN_POINT('Ctrl Pts',(19.1853171399678,5.95271794430234,6.04416714316602));
#157669=CARTESIAN_POINT('Ctrl Pts',(19.2087798990235,5.8774910195126,6.47128620995645));
#157670=CARTESIAN_POINT('Ctrl Pts',(19.2466843093111,5.86205261143494,7.14537690669814));
#157671=CARTESIAN_POINT('Ctrl Pts',(19.2604937503701,5.87727780168091,7.3883930320663));
#157672=CARTESIAN_POINT('Ctrl Pts',(19.3005707743551,5.98219667984587,8.09193506062706));
#157673=CARTESIAN_POINT('Ctrl Pts',(19.3260125741856,6.12710547128438,8.54054648012738));
#157674=CARTESIAN_POINT('Ctrl Pts',(19.3678816644823,6.46864618458046,9.20168746218623));
#157675=CARTESIAN_POINT('Ctrl Pts',(19.3835202161449,6.61876411563961,9.43393026367854));
#157676=CARTESIAN_POINT('Ctrl Pts',(19.414638151997,6.96381222178052,9.8687156698808));
#157677=CARTESIAN_POINT('Ctrl Pts',(19.4300392252702,7.15842094953444,10.0698209042673));
#157678=CARTESIAN_POINT('Ctrl Pts',(19.473442030871,7.75442043537448,10.5755628582299));
#157679=CARTESIAN_POINT('Ctrl Pts',(19.5020877234821,8.19201943815246,10.8303801925215));
#157680=CARTESIAN_POINT('Ctrl Pts',(19.5439781330779,8.89730494092279,11.0886021060379));
#157681=CARTESIAN_POINT('Ctrl Pts',(19.5576540928679,9.13777911174077,11.1534877285564));
#157682=CARTESIAN_POINT('Ctrl Pts',(19.5854375418345,9.6290530629089,11.2409219828863));
#157683=CARTESIAN_POINT('Ctrl Pts',(19.5996142344451,9.8789470933161,11.2629891261597));
#157684=CARTESIAN_POINT('Ctrl Pts',(19.6137437552536,10.1293149200936,11.2629999959823));
#157685=CARTESIAN_POINT('',(17.734,10.6581555755053,11.2300936493755));
#157686=CARTESIAN_POINT('Origin',(17.734,10.1295,7.));
#157687=CARTESIAN_POINT('Ctrl Pts',(17.734,10.6581555755053,11.2300936493755));
#157688=CARTESIAN_POINT('Ctrl Pts',(17.7616949897363,11.1488824019432,11.1687651081304));
#157689=CARTESIAN_POINT('Ctrl Pts',(17.7887411547574,11.6252164816622,11.0225101169825));
#157690=CARTESIAN_POINT('Ctrl Pts',(17.8283704905734,12.2488459039359,10.7045581296159));
#157691=CARTESIAN_POINT('Ctrl Pts',(17.840040605835,12.4248958275708,10.5981298986797));
#157692=CARTESIAN_POINT('Ctrl Pts',(17.8641028867666,12.77549500137,10.3499403602549));
#157693=CARTESIAN_POINT('Ctrl Pts',(17.8764490032863,12.9479121974887,10.206235555167));
#157694=CARTESIAN_POINT('Ctrl Pts',(17.9199030297306,13.5074194414442,9.65973748271246));
#157695=CARTESIAN_POINT('Ctrl Pts',(17.9515980360201,13.8261895030659,9.19522934563977));
#157696=CARTESIAN_POINT('Ctrl Pts',(17.9980916364257,14.1567255204859,8.42573715427207));
#157697=CARTESIAN_POINT('Ctrl Pts',(18.0135132032873,14.2415069949429,8.15873529814874));
#157698=CARTESIAN_POINT('Ctrl Pts',(18.0446456785229,14.356767835986,7.61585955813702));
#157699=CARTESIAN_POINT('Ctrl Pts',(18.0602767788215,14.3877260386578,7.34144189889881));
#157700=CARTESIAN_POINT('Ctrl Pts',(18.0972674830967,14.3978911621874,6.68465423453746));
#157701=CARTESIAN_POINT('Ctrl Pts',(18.1180690129512,14.3525994780205,6.30427024344823));
#157702=CARTESIAN_POINT('Ctrl Pts',(18.1543442829001,14.1906202473075,5.67645811688825));
#157703=CARTESIAN_POINT('Ctrl Pts',(18.16944942413,14.0997743614236,5.42476163756622));
#157704=CARTESIAN_POINT('Ctrl Pts',(18.2068329217642,13.8178295802788,4.82627311027319));
#157705=CARTESIAN_POINT('Ctrl Pts',(18.2284118162708,13.6009250725321,4.49439078429331));
#157706=CARTESIAN_POINT('Ctrl Pts',(18.2655893604534,13.1629216798711,3.99246341933803));
#157707=CARTESIAN_POINT('Ctrl Pts',(18.2809099585374,12.9652186480114,3.80537710443323));
#157708=CARTESIAN_POINT('Ctrl Pts',(18.3192591952197,12.4304752860569,3.38835543633559));
#157709=CARTESIAN_POINT('Ctrl Pts',(18.3415514937179,12.0757504454465,3.18547745510687));
#157710=CARTESIAN_POINT('Ctrl Pts',(18.3794657800805,11.4433735390018,2.93531061625104));
#157711=CARTESIAN_POINT('Ctrl Pts',(18.3948739914762,11.1799788566158,2.85941435868902));
#157712=CARTESIAN_POINT('Ctrl Pts',(18.4424275943522,10.3536066845282,2.70528145186069));
#157713=CARTESIAN_POINT('Ctrl Pts',(18.4731668243514,9.78087981819454,2.71359051196341));
#157714=CARTESIAN_POINT('Ctrl Pts',(18.518505973483,8.99449974862713,2.88401448716478));
#157715=CARTESIAN_POINT('Ctrl Pts',(18.5319909201975,8.76702457031755,2.95361613557958));
#157716=CARTESIAN_POINT('Ctrl Pts',(18.5686141586478,8.16162068842985,3.19572972788208));
#157717=CARTESIAN_POINT('Ctrl Pts',(18.5911937657581,7.80121566223636,3.40498683764839));
#157718=CARTESIAN_POINT('Ctrl Pts',(18.6291066957715,7.2730386993043,3.82486380705621));
#157719=CARTESIAN_POINT('Ctrl Pts',(18.6438750234105,7.08462699739337,4.0050699100077));
#157720=CARTESIAN_POINT('Ctrl Pts',(18.6734339719351,6.73987280833042,4.40119196250021));
#157721=CARTESIAN_POINT('Ctrl Pts',(18.6880123692262,6.58493645837877,4.61684085395999));
#157722=CARTESIAN_POINT('Ctrl Pts',(18.7336162491048,6.16995756759497,5.32534722466218));
#157723=CARTESIAN_POINT('Ctrl Pts',(18.7652059626455,5.98549365249281,5.85560035998954));
#157724=CARTESIAN_POINT('Ctrl Pts',(18.8116030190859,5.86912190868235,6.68305429248612));
#157725=CARTESIAN_POINT('Ctrl Pts',(18.8270172348669,5.85750963450242,6.96296049691824));
#157726=CARTESIAN_POINT('Ctrl Pts',(18.8583521429971,5.88922794992203,7.5208417297993));
#157727=CARTESIAN_POINT('Ctrl Pts',(18.8741990497534,5.9324506783649,7.79746776882433));
#157728=CARTESIAN_POINT('Ctrl Pts',(18.9167047062517,6.12147134216349,8.52799592711725));
#157729=CARTESIAN_POINT('Ctrl Pts',(18.9425081610268,6.31664167906196,8.96498829608126));
#157730=CARTESIAN_POINT('Ctrl Pts',(18.9829337727668,6.71411921308159,9.56264230070435));
#157731=CARTESIAN_POINT('Ctrl Pts',(18.9967032709609,6.86537344567519,9.75271471476632));
#157732=CARTESIAN_POINT('Ctrl Pts',(19.0341600899032,7.3234092395884,10.2371236706298));
#157733=CARTESIAN_POINT('Ctrl Pts',(19.0572543340028,7.65923372746821,10.5001293577879));
#157734=CARTESIAN_POINT('Ctrl Pts',(19.0957939377919,8.25570526069354,10.8380136743055));
#157735=CARTESIAN_POINT('Ctrl Pts',(19.1106329303094,8.49443402195775,10.9456320449966));
#157736=CARTESIAN_POINT('Ctrl Pts',(19.1519247463186,9.18867344018609,11.1846962566353));
#157737=CARTESIAN_POINT('Ctrl Pts',(19.1775909397056,9.65778711534599,11.263000043841));
#157738=CARTESIAN_POINT('Ctrl Pts',(19.2041804397713,10.1295003962029,11.263));
#157739=CARTESIAN_POINT('Origin',(23.734,10.1295,7.));
#157740=CARTESIAN_POINT('',(21.113681670589,10.1298201264287,11.2629999879802));
#157741=CARTESIAN_POINT('',(20.7043183294109,10.1330470789259,11.2629985243055));
#157742=CARTESIAN_POINT('',(23.734,10.1295,11.263));
#157743=CARTESIAN_POINT('Ctrl Pts',(19.613681670589,10.1293184243372,11.262999996133));
#157744=CARTESIAN_POINT('Ctrl Pts',(19.6210623037642,10.2610687195736,11.263005607826));
#157745=CARTESIAN_POINT('Ctrl Pts',(19.6284429369393,10.3928267771473,11.2568991564636));
#157746=CARTESIAN_POINT('Ctrl Pts',(19.6358235701145,10.5240278125494,11.2447045604052));
#157747=CARTESIAN_POINT('Ctrl Pts',(19.6432028342893,10.6552045120622,11.2325122262675));
#157748=CARTESIAN_POINT('Ctrl Pts',(19.650582098464,10.7858240783452,11.2142340323102));
#157749=CARTESIAN_POINT('Ctrl Pts',(19.6579613626388,10.9153264213143,11.1899458034161));
#157750=CARTESIAN_POINT('Ctrl Pts',(19.6653396985726,11.044812474126,11.1656606297492));
#157751=CARTESIAN_POINT('Ctrl Pts',(19.6727180345064,11.1731812706445,11.1353669878975));
#157752=CARTESIAN_POINT('Ctrl Pts',(19.6800963704403,11.2998820511657,11.0991919757812));
#157753=CARTESIAN_POINT('Ctrl Pts',(19.6849288196367,11.382864866059,11.0754991119973));
#157754=CARTESIAN_POINT('Ctrl Pts',(19.6897612688331,11.4651323638681,11.0492844183613));
#157755=CARTESIAN_POINT('Ctrl Pts',(19.6945937180296,11.5465329042847,11.0205953226076));
#157756=CARTESIAN_POINT('Ctrl Pts',(19.7016231773756,11.6649411412557,10.9788631027588));
#157757=CARTESIAN_POINT('Ctrl Pts',(19.7086526367216,11.7815525661295,10.9318790465684));
#157758=CARTESIAN_POINT('Ctrl Pts',(19.7156820960676,11.8958854944383,10.8798261926326));
#157759=CARTESIAN_POINT('Ctrl Pts',(19.722709782053,12.0101895793458,10.8277864703587));
#157760=CARTESIAN_POINT('Ctrl Pts',(19.7297374680383,12.1222159630139,10.7706806571767));
#157761=CARTESIAN_POINT('Ctrl Pts',(19.7367651540237,12.2315037832726,10.7087395561171));
#157762=CARTESIAN_POINT('Ctrl Pts',(19.7437942650805,12.3408137648732,10.6467858946649));
#157763=CARTESIAN_POINT('Ctrl Pts',(19.7508233761373,12.4473837362772,10.5799951717423));
#157764=CARTESIAN_POINT('Ctrl Pts',(19.7578524871941,12.5507782076321,10.5086437324479));
#157765=CARTESIAN_POINT('Ctrl Pts',(19.7648822673835,12.6541825215712,10.4372855008895));
#157766=CARTESIAN_POINT('Ctrl Pts',(19.771912047573,12.7544104201016,10.3613659117439));
#157767=CARTESIAN_POINT('Ctrl Pts',(19.7789418277624,12.8510567997471,10.2812036794065));
#157768=CARTESIAN_POINT('Ctrl Pts',(19.7859761861195,12.947766120667,10.20098924115));
#157769=CARTESIAN_POINT('Ctrl Pts',(19.7930105444766,13.0408889712832,10.116526891086));
#157770=CARTESIAN_POINT('Ctrl Pts',(19.8000449028336,13.1300544842105,10.0281746626118));
#157771=CARTESIAN_POINT('Ctrl Pts',(19.803676389535,13.176086170113,9.9825628347157));
#157772=CARTESIAN_POINT('Ctrl Pts',(19.8073078762364,13.2210637677684,9.93591490652767));
#157773=CARTESIAN_POINT('Ctrl Pts',(19.8109393629378,13.2649402640227,9.88828380716734));
#157774=CARTESIAN_POINT('Ctrl Pts',(19.8185510511639,13.3569065129464,9.788447814911));
#157775=CARTESIAN_POINT('Ctrl Pts',(19.82616273939,13.4440921851538,9.68422623732347));
#157776=CARTESIAN_POINT('Ctrl Pts',(19.8337744276161,13.5261126987745,9.57608058385672));
#157777=CARTESIAN_POINT('Ctrl Pts',(19.8415669759686,13.6100820889147,9.46536529853304));
#157778=CARTESIAN_POINT('Ctrl Pts',(19.8493595243211,13.6886375971267,9.350537337596));
#157779=CARTESIAN_POINT('Ctrl Pts',(19.8571520726736,13.7614114960694,9.23212631468719));
#157780=CARTESIAN_POINT('Ctrl Pts',(19.8647577752929,13.8324404597364,9.11655449063818));
#157781=CARTESIAN_POINT('Ctrl Pts',(19.8723634779121,13.8979617722854,8.99756971412403));
#157782=CARTESIAN_POINT('Ctrl Pts',(19.8799691805314,13.9576776738065,8.87569312462606));
#157783=CARTESIAN_POINT('Ctrl Pts',(19.8878551517505,14.0195940941942,8.74932540750959));
#157784=CARTESIAN_POINT('Ctrl Pts',(19.8957411229696,14.0752688994055,8.61984891580091));
#157785=CARTESIAN_POINT('Ctrl Pts',(19.9036270941887,14.1244221857155,8.48787288774221));
#157786=CARTESIAN_POINT('Ctrl Pts',(19.9115130654078,14.1735754720254,8.35589685968352));
#157787=CARTESIAN_POINT('Ctrl Pts',(19.9193990366269,14.2162070893851,8.22142157961869));
#157788=CARTESIAN_POINT('Ctrl Pts',(19.9272850078459,14.2520924147731,8.08508100234748));
#157789=CARTESIAN_POINT('Ctrl Pts',(19.9343239536661,14.2841233281666,7.9633846494403));
#157790=CARTESIAN_POINT('Ctrl Pts',(19.9413628994862,14.3107676181272,7.8402454199408));
#157791=CARTESIAN_POINT('Ctrl Pts',(19.9484018453063,14.3319126474473,7.71616823482706));
#157792=CARTESIAN_POINT('Ctrl Pts',(19.9554405817332,14.3530570477492,7.59209474073655));
#157793=CARTESIAN_POINT('Ctrl Pts',(19.9624793181602,14.3687024503286,7.4670837237731));
#157794=CARTESIAN_POINT('Ctrl Pts',(19.9695180545871,14.3787875954937,7.34164884133137));
#157795=CARTESIAN_POINT('Ctrl Pts',(19.976560483799,14.3888780317039,7.21614815104951));
#157796=CARTESIAN_POINT('Ctrl Pts',(19.9836029130109,14.3934023507515,7.09022353254098));
#157797=CARTESIAN_POINT('Ctrl Pts',(19.9906453422228,14.3923512886368,6.96439254336727));
#157798=CARTESIAN_POINT('Ctrl Pts',(19.9976897288499,14.3912999343835,6.83852657996872));
#157799=CARTESIAN_POINT('Ctrl Pts',(20.0047341154771,14.384670122848,6.71275468020004));
#157800=CARTESIAN_POINT('Ctrl Pts',(20.0117785021043,14.3725046893258,6.58759218441076));
#157801=CARTESIAN_POINT('Ctrl Pts',(20.0188293217025,14.3603281462655,6.46231538956881));
#157802=CARTESIAN_POINT('Ctrl Pts',(20.0258801413008,14.3426059296771,6.33764949029167));
#157803=CARTESIAN_POINT('Ctrl Pts',(20.032930960899,14.3194325420246,6.21410287360031));
#157804=CARTESIAN_POINT('Ctrl Pts',(20.0364975248507,14.3077105900036,6.15160844961165));
#157805=CARTESIAN_POINT('Ctrl Pts',(20.0400640888024,14.2945946542908,6.08940024916908));
#157806=CARTESIAN_POINT('Ctrl Pts',(20.043630652754,14.2801018815878,6.02754279242752));
#157807=CARTESIAN_POINT('Ctrl Pts',(20.0506540757907,14.2515621231407,5.9057305685185));
#157808=CARTESIAN_POINT('Ctrl Pts',(20.0576774988273,14.2176287610004,5.78506067889005));
#157809=CARTESIAN_POINT('Ctrl Pts',(20.064700921864,14.178413687597,5.66603337733305));
#157810=CARTESIAN_POINT('Ctrl Pts',(20.0717185186296,14.1392311450044,5.54710481471211));
#157811=CARTESIAN_POINT('Ctrl Pts',(20.0787361153952,14.0947757355895,5.42981649293811));
#157812=CARTESIAN_POINT('Ctrl Pts',(20.0857537121608,14.0452096568303,5.31465526274116));
#157813=CARTESIAN_POINT('Ctrl Pts',(20.0927670515899,13.9956736481201,5.19956389693379));
#157814=CARTESIAN_POINT('Ctrl Pts',(20.0997803910189,13.9410332971071,5.08659740716836));
#157815=CARTESIAN_POINT('Ctrl Pts',(20.106793730448,13.8814994526977,4.97622404724333));
#157816=CARTESIAN_POINT('Ctrl Pts',(20.1138574059531,13.821538322521,4.86505851664211));
#157817=CARTESIAN_POINT('Ctrl Pts',(20.1209210814582,13.7566133174844,4.75652385852162));
#157818=CARTESIAN_POINT('Ctrl Pts',(20.1279847569633,13.6869877988477,4.65107480726828));
#157819=CARTESIAN_POINT('Ctrl Pts',(20.1349957098057,13.6178819590572,4.54641281860872));
#157820=CARTESIAN_POINT('Ctrl Pts',(20.1420066626481,13.5441457768754,4.4447908421696));
#157821=CARTESIAN_POINT('Ctrl Pts',(20.1490176154904,13.4660808058284,4.34662525711552));
#157822=CARTESIAN_POINT('Ctrl Pts',(20.1560292419106,13.3880083346838,4.24845024079589));
#157823=CARTESIAN_POINT('Ctrl Pts',(20.1630408683308,13.3056064871499,4.15373257998509));
#157824=CARTESIAN_POINT('Ctrl Pts',(20.1700524947509,13.2192173973556,4.06285591016064));
#157825=CARTESIAN_POINT('Ctrl Pts',(20.1770662121528,13.1328025449214,3.97195213942652));
#157826=CARTESIAN_POINT('Ctrl Pts',(20.1840799295547,13.0423983490892,3.8848919206958));
#157827=CARTESIAN_POINT('Ctrl Pts',(20.1910936469566,12.9483838509154,3.80202207089415));
#157828=CARTESIAN_POINT('Ctrl Pts',(20.1981960049244,12.8531811813556,3.71810489768801));
#157829=CARTESIAN_POINT('Ctrl Pts',(20.2052983628922,12.7542766304511,3.63848501133126));
#157830=CARTESIAN_POINT('Ctrl Pts',(20.2124007208601,12.6520974127302,3.56347976969624));
#157831=CARTESIAN_POINT('Ctrl Pts',(20.2194266380452,12.5510179226514,3.48928178945322));
#157832=CARTESIAN_POINT('Ctrl Pts',(20.2264525552303,12.4467342673697,3.41959977243168));
#157833=CARTESIAN_POINT('Ctrl Pts',(20.2334784724154,12.3396876781542,3.35469625033312));
#157834=CARTESIAN_POINT('Ctrl Pts',(20.2406190507746,12.2308941159415,3.28873351932974));
#157835=CARTESIAN_POINT('Ctrl Pts',(20.2477596291338,12.1192470170137,3.22770681705742));
#157836=CARTESIAN_POINT('Ctrl Pts',(20.254900207493,12.0052331387805,3.17184193219762));
#157837=CARTESIAN_POINT('Ctrl Pts',(20.2620407858522,11.8912192605474,3.11597704733782));
#157838=CARTESIAN_POINT('Ctrl Pts',(20.2691813642114,11.7748390041325,3.06527409536859));
#157839=CARTESIAN_POINT('Ctrl Pts',(20.2763219425706,11.6565970046819,3.01990656663797));
#157840=CARTESIAN_POINT('Ctrl Pts',(20.2831124368812,11.5441521039813,2.97676329024846));
#157841=CARTESIAN_POINT('Ctrl Pts',(20.2899029311918,11.4296496272437,2.93830180029273));
#157842=CARTESIAN_POINT('Ctrl Pts',(20.2966934255024,11.3135242806343,2.90472766438319));
#157843=CARTESIAN_POINT('Ctrl Pts',(20.3034747086535,11.1975564555602,2.87119907106695));
#157844=CARTESIAN_POINT('Ctrl Pts',(20.3102559918046,11.0799705337984,2.84254477101641));
#157845=CARTESIAN_POINT('Ctrl Pts',(20.3170372749558,10.9612220024664,2.81892268540592));
#157846=CARTESIAN_POINT('Ctrl Pts',(20.3238112366047,10.8426016795597,2.79532610369315));
#157847=CARTESIAN_POINT('Ctrl Pts',(20.3305851982536,10.7228216505048,2.77675101741854));
#157848=CARTESIAN_POINT('Ctrl Pts',(20.3373591599025,10.602352688061,2.76330561222627));
#157849=CARTESIAN_POINT('Ctrl Pts',(20.3441276801126,10.48198049683,2.74987100756003));
#157850=CARTESIAN_POINT('Ctrl Pts',(20.3508962003228,10.3609208876254,2.74155793704571));
#157851=CARTESIAN_POINT('Ctrl Pts',(20.3576647205329,10.2396542166227,2.73842340810819));
#157852=CARTESIAN_POINT('Ctrl Pts',(20.3644304116747,10.1184382319863,2.73529018932358));
#157853=CARTESIAN_POINT('Ctrl Pts',(20.3711961028166,9.99701577598613,2.73733122414958));
#157854=CARTESIAN_POINT('Ctrl Pts',(20.3779617939584,9.8758711148973,2.74455156433055));
#157855=CARTESIAN_POINT('Ctrl Pts',(20.3847262515225,9.7547485419237,2.75177058803827));
#157856=CARTESIAN_POINT('Ctrl Pts',(20.3914907090865,9.63390408190446,2.76416701590755));
#157857=CARTESIAN_POINT('Ctrl Pts',(20.3982551666505,9.51381996728511,2.78169381181069));
#157858=CARTESIAN_POINT('Ctrl Pts',(20.4050200814275,9.39372773612192,2.79922179235852));
#157859=CARTESIAN_POINT('Ctrl Pts',(20.4117849962045,9.27439636769387,2.82188076925702));
#157860=CARTESIAN_POINT('Ctrl Pts',(20.4185499109815,9.15630016132667,2.8495721818099));
#157861=CARTESIAN_POINT('Ctrl Pts',(20.4253169740298,9.03816645224213,2.87727238806794));
#157862=CARTESIAN_POINT('Ctrl Pts',(20.4320840370781,8.92126909293508,2.91000810994903));
#157863=CARTESIAN_POINT('Ctrl Pts',(20.4388511001264,8.8060686569394,2.94763051040446));
#157864=CARTESIAN_POINT('Ctrl Pts',(20.4456261525318,8.69073221254255,2.98529732876934));
#157865=CARTESIAN_POINT('Ctrl Pts',(20.4524012049372,8.57709708877692,3.02786220934678));
#157866=CARTESIAN_POINT('Ctrl Pts',(20.4591762573426,8.46560533251585,3.07512757716664));
#157867=CARTESIAN_POINT('Ctrl Pts',(20.465955865875,8.3540385996251,3.12242473027806));
#157868=CARTESIAN_POINT('Ctrl Pts',(20.4727354744074,8.24461847941592,3.17442847978152));
#157869=CARTESIAN_POINT('Ctrl Pts',(20.4795150829397,8.13776210427539,3.23089544391052));
#157870=CARTESIAN_POINT('Ctrl Pts',(20.4863055094517,8.03073522222619,3.28745251036128));
#157871=CARTESIAN_POINT('Ctrl Pts',(20.4930959359638,7.92628060892515,3.34848679214083));
#157872=CARTESIAN_POINT('Ctrl Pts',(20.4998863624758,7.82478626913523,3.41371172118535));
#157873=CARTESIAN_POINT('Ctrl Pts',(20.5029286524462,7.77931413105292,3.44293420774036));
#157874=CARTESIAN_POINT('Ctrl Pts',(20.5059709424165,7.73443575525086,3.4729973349816));
#157875=CARTESIAN_POINT('Ctrl Pts',(20.5090132323869,7.69018375192213,3.50387282241288));
#157876=CARTESIAN_POINT('Ctrl Pts',(20.5160528480572,7.58778815547792,3.57531623091908));
#157877=CARTESIAN_POINT('Ctrl Pts',(20.5230924637274,7.48839576824068,3.65135791091549));
#157878=CARTESIAN_POINT('Ctrl Pts',(20.5301320793977,7.39243615095284,3.73172056178803));
#157879=CARTESIAN_POINT('Ctrl Pts',(20.5371627089137,7.29659902727188,3.81198062876912));
#157880=CARTESIAN_POINT('Ctrl Pts',(20.5441933384298,7.20418624476916,3.89655044007299));
#157881=CARTESIAN_POINT('Ctrl Pts',(20.5512239679459,7.11559764941311,3.98511001508732));
#157882=CARTESIAN_POINT('Ctrl Pts',(20.5582471924636,7.0271023598425,4.07357631488181));
#157883=CARTESIAN_POINT('Ctrl Pts',(20.5652704169812,6.94242351009667,4.16602373977542));
#157884=CARTESIAN_POINT('Ctrl Pts',(20.5722936414989,6.86192690158119,4.26209294414699));
#157885=CARTESIAN_POINT('Ctrl Pts',(20.5793524281949,6.78102269755993,4.3586485960431));
#157886=CARTESIAN_POINT('Ctrl Pts',(20.5864112148909,6.70434351288937,4.45886255685475));
#157887=CARTESIAN_POINT('Ctrl Pts',(20.5934700015869,6.63222286897191,4.56233274034623));
#157888=CARTESIAN_POINT('Ctrl Pts',(20.6004830794517,6.56056923879038,4.66513290767694));
#157889=CARTESIAN_POINT('Ctrl Pts',(20.6074961573164,6.49341550627245,4.77114692695205));
#157890=CARTESIAN_POINT('Ctrl Pts',(20.6145092351811,6.4310476922353,4.87994822535157));
#157891=CARTESIAN_POINT('Ctrl Pts',(20.6215200654578,6.36869986616283,4.9887146545394));
#157892=CARTESIAN_POINT('Ctrl Pts',(20.6285308957345,6.31113509680343,5.10026624921301));
#157893=CARTESIAN_POINT('Ctrl Pts',(20.6355417260111,6.25859484105923,5.21414943220723));
#157894=CARTESIAN_POINT('Ctrl Pts',(20.6425517265455,6.20606080353314,5.32801913695587));
#157895=CARTESIAN_POINT('Ctrl Pts',(20.6495617270799,6.15855025661158,5.44421952922821));
#157896=CARTESIAN_POINT('Ctrl Pts',(20.6565717276143,6.11625749444774,5.56227485532575));
#157897=CARTESIAN_POINT('Ctrl Pts',(20.6636661271634,6.07345553582416,5.68175154411103));
#157898=CARTESIAN_POINT('Ctrl Pts',(20.6707605267125,6.0359979916284,5.80312775504321));
#157899=CARTESIAN_POINT('Ctrl Pts',(20.6778549262616,6.00403488298935,5.92589266442861));
#157900=CARTESIAN_POINT('Ctrl Pts',(20.6848699695753,5.97242930594331,6.04728435526654));
#157901=CARTESIAN_POINT('Ctrl Pts',(20.691885012889,5.94619591700699,6.17003344375839));
#157902=CARTESIAN_POINT('Ctrl Pts',(20.6989000562027,5.92542852701159,6.29363462004067));
#157903=CARTESIAN_POINT('Ctrl Pts',(20.7060341338695,5.90430874677111,6.41933311566898));
#157904=CARTESIAN_POINT('Ctrl Pts',(20.7131682115363,5.88884222559255,6.54591246948119));
#157905=CARTESIAN_POINT('Ctrl Pts',(20.720302289203,5.87907269796409,6.67283528596788));
#157906=CARTESIAN_POINT('Ctrl Pts',(20.7274363668698,5.86930317033562,6.79975810245456));
#157907=CARTESIAN_POINT('Ctrl Pts',(20.7345704445365,5.86523062067719,6.92702396271638));
#157908=CARTESIAN_POINT('Ctrl Pts',(20.7417045222033,5.86684324052786,7.05409575700999));
#157909=CARTESIAN_POINT('Ctrl Pts',(20.7487555408127,5.86843708532577,7.17968810799774));
#157910=CARTESIAN_POINT('Ctrl Pts',(20.7558065594222,5.87558719238043,7.30531726205016));
#157911=CARTESIAN_POINT('Ctrl Pts',(20.7628575780316,5.88828942330491,7.43046700701646));
#157912=CARTESIAN_POINT('Ctrl Pts',(20.7699032665315,5.90098205217249,7.55552214695005));
#157913=CARTESIAN_POINT('Ctrl Pts',(20.7769489550314,5.91921840902034,7.68009822009394));
#157914=CARTESIAN_POINT('Ctrl Pts',(20.7839946435314,5.94294234854903,7.80368154829967));
#157915=CARTESIAN_POINT('Ctrl Pts',(20.7910363483395,5.96665287436202,7.92719500144824));
#157916=CARTESIAN_POINT('Ctrl Pts',(20.7980780531477,5.99584473055009,8.04971645279611));
#157917=CARTESIAN_POINT('Ctrl Pts',(20.8051197579558,6.03041028946687,8.17074016972232));
#157918=CARTESIAN_POINT('Ctrl Pts',(20.8121590390629,6.06496395118215,8.29172223120907));
#157919=CARTESIAN_POINT('Ctrl Pts',(20.81919832017,6.10488752575289,8.41120721791972));
#157920=CARTESIAN_POINT('Ctrl Pts',(20.8262376012772,6.15002298728712,8.528702621601));
#157921=CARTESIAN_POINT('Ctrl Pts',(20.8332767281295,6.19515745974894,8.64619545055594));
#157922=CARTESIAN_POINT('Ctrl Pts',(20.8403158549819,6.24550345864841,8.76169842478665));
#157923=CARTESIAN_POINT('Ctrl Pts',(20.8473549818343,6.30085412572507,8.87473725342982));
#157924=CARTESIAN_POINT('Ctrl Pts',(20.8509200435934,6.32888722566361,8.93198730925843));
#157925=CARTESIAN_POINT('Ctrl Pts',(20.8544851053524,6.35820328570989,8.98860562121714));
#157926=CARTESIAN_POINT('Ctrl Pts',(20.8580501671115,6.38877083910759,9.04453279378179));
#157927=CARTESIAN_POINT('Ctrl Pts',(20.8656419313286,6.45386414569605,9.16362916184931));
#157928=CARTESIAN_POINT('Ctrl Pts',(20.8732336955456,6.52461037034493,9.27954435589301));
#157929=CARTESIAN_POINT('Ctrl Pts',(20.8808254597627,6.60067979658225,9.39177694862015));
#157930=CARTESIAN_POINT('Ctrl Pts',(20.8886229891175,6.67881098811066,9.50705146338693));
#157931=CARTESIAN_POINT('Ctrl Pts',(20.8964205184722,6.7625578532525,9.61844067454016));
#157932=CARTESIAN_POINT('Ctrl Pts',(20.904218047827,6.85151803388108,9.72543633750618));
#157933=CARTESIAN_POINT('Ctrl Pts',(20.9118262952094,6.93831874095385,9.82983472264376));
#157934=CARTESIAN_POINT('Ctrl Pts',(20.9194345425919,7.03008237539708,9.93005022576152));
#157935=CARTESIAN_POINT('Ctrl Pts',(20.9270427899744,7.12639604911989,10.0256463210706));
#157936=CARTESIAN_POINT('Ctrl Pts',(20.9349349603153,7.22630393604349,10.1248098511419));
#157937=CARTESIAN_POINT('Ctrl Pts',(20.9428271306562,7.3311078117208,10.219002308715));
#157938=CARTESIAN_POINT('Ctrl Pts',(20.950719300997,7.4403062336633,10.3077796007437));
#157939=CARTESIAN_POINT('Ctrl Pts',(20.9586114713379,7.5495046556058,10.3965568927723));
#157940=CARTESIAN_POINT('Ctrl Pts',(20.9665036416788,7.66309737480791,10.4799188219024));
#157941=CARTESIAN_POINT('Ctrl Pts',(20.9743958120197,7.78054523318155,10.5574682716));
#157942=CARTESIAN_POINT('Ctrl Pts',(20.9814302636453,7.88522889338838,10.6265896702683));
#157943=CARTESIAN_POINT('Ctrl Pts',(20.9884647152709,7.99303771031586,10.6911341334027));
#157944=CARTESIAN_POINT('Ctrl Pts',(20.9954991668964,8.10354027043256,10.750820733409));
#157945=CARTESIAN_POINT('Ctrl Pts',(21.0025297316031,8.2139817718456,10.8104743533069));
#157946=CARTESIAN_POINT('Ctrl Pts',(21.0095602963097,8.32711371454162,10.8652752730648));
#157947=CARTESIAN_POINT('Ctrl Pts',(21.0165908610163,8.44247818970125,10.9149874088656));
#157948=CARTESIAN_POINT('Ctrl Pts',(21.0236196792195,8.55781400650079,10.9646871953857));
#157949=CARTESIAN_POINT('Ctrl Pts',(21.0306484974226,8.67538089984565,11.0093005597809));
#157950=CARTESIAN_POINT('Ctrl Pts',(21.0376773156258,8.79469914404457,11.0486387434471));
#157951=CARTESIAN_POINT('Ctrl Pts',(21.0447049946651,8.91399805027931,11.0879705515553));
#157952=CARTESIAN_POINT('Ctrl Pts',(21.0517326737043,9.03504737574514,11.1220287644151));
#157953=CARTESIAN_POINT('Ctrl Pts',(21.0587603527436,9.15735080920185,11.1506740357237));
#157954=CARTESIAN_POINT('Ctrl Pts',(21.0657898849612,9.27968649371527,11.1793268607063));
#157955=CARTESIAN_POINT('Ctrl Pts',(21.0728194171789,9.40327657205448,11.2025638053603));
#157956=CARTESIAN_POINT('Ctrl Pts',(21.0798489493965,9.52761306300916,11.220296330245));
#157957=CARTESIAN_POINT('Ctrl Pts',(21.0834797852403,9.59183431900078,11.2294553873429));
#157958=CARTESIAN_POINT('Ctrl Pts',(21.0871106210841,9.65625455719416,11.2371467896353));
#157959=CARTESIAN_POINT('Ctrl Pts',(21.0907414569279,9.7208031090756,11.2433637425218));
#157960=CARTESIAN_POINT('Ctrl Pts',(21.0983881948149,9.8567458722469,11.2564569836444));
#157961=CARTESIAN_POINT('Ctrl Pts',(21.106034932702,9.99328288766813,11.2630102411303));
#157962=CARTESIAN_POINT('Ctrl Pts',(21.113681670589,10.1298201264287,11.2629999879802));
#157963=CARTESIAN_POINT('Ctrl Pts',(19.2041804397713,10.1295003962029,11.263));
#157964=CARTESIAN_POINT('Ctrl Pts',(19.2091555282883,10.2177613759535,11.262999991797));
#157965=CARTESIAN_POINT('Ctrl Pts',(19.2141496156627,10.3061141204568,11.2602590201419));
#157966=CARTESIAN_POINT('Ctrl Pts',(19.2344704543066,10.6646652801004,11.2379329571964));
#157967=CARTESIAN_POINT('Ctrl Pts',(19.2496908524141,10.9326920234655,11.1953988307096));
#157968=CARTESIAN_POINT('Ctrl Pts',(19.2797046258122,11.4565285457862,11.0601954318409));
#157969=CARTESIAN_POINT('Ctrl Pts',(19.2946346817085,11.7111627636934,10.9679378982786));
#157970=CARTESIAN_POINT('Ctrl Pts',(19.3315996560539,12.3063541787618,10.6858325829712));
#157971=CARTESIAN_POINT('Ctrl Pts',(19.3536978982461,12.6329899403981,10.4722627163212));
#157972=CARTESIAN_POINT('Ctrl Pts',(19.3877230669708,13.0950538749999,10.0706235651989));
#157973=CARTESIAN_POINT('Ctrl Pts',(19.4000640296122,13.2521141818841,9.91075924709942));
#157974=CARTESIAN_POINT('Ctrl Pts',(19.4357312298586,13.6630070448086,9.4208033139932));
#157975=CARTESIAN_POINT('Ctrl Pts',(19.4593953461805,13.8820913705074,9.06494763762778));
#157976=CARTESIAN_POINT('Ctrl Pts',(19.4958359772684,14.1395982420948,8.46569002107918));
#157977=CARTESIAN_POINT('Ctrl Pts',(19.5088553757794,14.2147436659343,8.24093608349154));
#157978=CARTESIAN_POINT('Ctrl Pts',(19.5535545931509,14.4053393872225,7.46028346490425));
#157979=CARTESIAN_POINT('Ctrl Pts',(19.5857136184606,14.4285872270892,6.88812837299951));
#157980=CARTESIAN_POINT('Ctrl Pts',(19.6323168676482,14.2961534186914,6.05824455511635));
#157981=CARTESIAN_POINT('Ctrl Pts',(19.6474533909766,14.2272056986917,5.79305876366753));
#157982=CARTESIAN_POINT('Ctrl Pts',(19.6857684809327,13.9932393926121,5.15305688632271));
#157983=CARTESIAN_POINT('Ctrl Pts',(19.7088876903985,13.7988236342008,4.79188655028604));
#157984=CARTESIAN_POINT('Ctrl Pts',(19.7465531814489,13.3946263547052,4.24577739348952));
#157985=CARTESIAN_POINT('Ctrl Pts',(19.7615465917255,13.2127536149457,4.04359417204778));
#157986=CARTESIAN_POINT('Ctrl Pts',(19.798491640212,12.7280248607654,3.59846612441179));
#157987=CARTESIAN_POINT('Ctrl Pts',(19.8204785529977,12.408856941812,3.37683700633801));
#157988=CARTESIAN_POINT('Ctrl Pts',(19.8566610655473,11.8289531070741,3.08149027174962));
#157989=CARTESIAN_POINT('Ctrl Pts',(19.8712342531552,11.58309787199,2.98379394328921));
#157990=CARTESIAN_POINT('Ctrl Pts',(19.9082163625415,10.9497473469888,2.7979489841858));
#157991=CARTESIAN_POINT('Ctrl Pts',(19.9307842906331,10.5560084986188,2.73993671915285));
#157992=CARTESIAN_POINT('Ctrl Pts',(19.9695236866791,9.85941229810532,2.73496282863175));
#157993=CARTESIAN_POINT('Ctrl Pts',(19.9860035798403,9.55950248987418,2.76460233010767));
#157994=CARTESIAN_POINT('Ctrl Pts',(20.0229371076307,8.91280204416998,2.8984967389742));
#157995=CARTESIAN_POINT('Ctrl Pts',(20.0434322172209,8.57105887634374,3.01578895256602));
#157996=CARTESIAN_POINT('Ctrl Pts',(20.0769000040484,8.03479136220468,3.27953142000264));
#157997=CARTESIAN_POINT('Ctrl Pts',(20.0900163507226,7.83060149372497,3.40211734388238));
#157998=CARTESIAN_POINT('Ctrl Pts',(20.1338095512129,7.19270610888212,3.86165767663712));
#157999=CARTESIAN_POINT('Ctrl Pts',(20.1648930200309,6.81373218408336,4.26510658271138));
#158000=CARTESIAN_POINT('Ctrl Pts',(20.2103643554928,6.37698899278802,4.95903584802513));
#158001=CARTESIAN_POINT('Ctrl Pts',(20.2253878983731,6.25466168325506,5.20208544273264));
#158002=CARTESIAN_POINT('Ctrl Pts',(20.265076338985,5.99911605061139,5.85930905056656));
#158003=CARTESIAN_POINT('Ctrl Pts',(20.2897711795976,5.90453976302446,6.28515777739997));
#158004=CARTESIAN_POINT('Ctrl Pts',(20.3258939710697,5.86107099681106,6.94068417744711));
#158005=CARTESIAN_POINT('Ctrl Pts',(20.3380665169335,5.86381992540913,7.16424877544068));
#158006=CARTESIAN_POINT('Ctrl Pts',(20.371741745925,5.91913743472679,7.77176835866281));
#158007=CARTESIAN_POINT('Ctrl Pts',(20.3934865621156,6.00647306353156,8.15038990357501));
#158008=CARTESIAN_POINT('Ctrl Pts',(20.4455102960916,6.33112460849197,9.0062184383894));
#158009=CARTESIAN_POINT('Ctrl Pts',(20.4764801611693,6.60887478254657,9.46123463933842));
#158010=CARTESIAN_POINT('Ctrl Pts',(20.5119580174849,7.02483927015239,9.92281955521915));
#158011=CARTESIAN_POINT('Ctrl Pts',(20.5172006914584,7.08924585716699,9.98975731009913));
#158012=CARTESIAN_POINT('Ctrl Pts',(20.5267183602449,7.2124004403559,10.1096529137158));
#158013=CARTESIAN_POINT('Ctrl Pts',(20.5310107442253,7.27052964225416,10.1631789130787));
#158014=CARTESIAN_POINT('Ctrl Pts',(20.5484386539012,7.51696918442732,10.3777554714386));
#158015=CARTESIAN_POINT('Ctrl Pts',(20.5609307880345,7.71765784539843,10.523859312996));
#158016=CARTESIAN_POINT('Ctrl Pts',(20.5854393461132,8.12956102938122,10.7719668847095));
#158017=CARTESIAN_POINT('Ctrl Pts',(20.5974044794598,8.33871786847911,10.8756388895332));
#158018=CARTESIAN_POINT('Ctrl Pts',(20.6150536709055,8.64443499427547,10.9971180667588));
#158019=CARTESIAN_POINT('Ctrl Pts',(20.6202822909967,8.73474679395746,11.0295201389533));
#158020=CARTESIAN_POINT('Ctrl Pts',(20.6304484270141,8.90909128553992,11.0855079059924));
#158021=CARTESIAN_POINT('Ctrl Pts',(20.635366617745,8.99290606745967,11.1096137248184));
#158022=CARTESIAN_POINT('Ctrl Pts',(20.6478456224131,9.20384891131824,11.1633359546457));
#158023=CARTESIAN_POINT('Ctrl Pts',(20.6555008505231,9.3317021745655,11.1897147616175));
#158024=CARTESIAN_POINT('Ctrl Pts',(20.6767866376051,9.68298663275184,11.245529383248));
#158025=CARTESIAN_POINT('Ctrl Pts',(20.6907029872948,9.90784737756346,11.26318471361));
#158026=CARTESIAN_POINT('Ctrl Pts',(20.7046814563364,10.1330245361105,11.2629985430029));
#158027=CARTESIAN_POINT('Origin',(23.734,10.1295,7.));
#158028=CARTESIAN_POINT('',(22.6135314140065,10.129499907926,11.263));
#158029=CARTESIAN_POINT('',(22.2043183294109,10.1294634642048,11.2629999998434));
#158030=CARTESIAN_POINT('',(23.734,10.1295,11.263));
#158031=CARTESIAN_POINT('Ctrl Pts',(22.6135314140065,10.129499907926,11.263));
#158032=CARTESIAN_POINT('Ctrl Pts',(22.6114428647833,10.0924740380264,11.2629999992003));
#158033=CARTESIAN_POINT('Ctrl Pts',(22.609356796018,10.0554407197264,11.2625176221842));
#158034=CARTESIAN_POINT('Ctrl Pts',(22.5828597608454,9.58418469426959,11.2502328609711));
#158035=CARTESIAN_POINT('Ctrl Pts',(22.5592247311594,9.15423404753517,11.1726142704355));
#158036=CARTESIAN_POINT('Ctrl Pts',(22.5159780879935,8.4271237417952,10.9226239895735));
#158037=CARTESIAN_POINT('Ctrl Pts',(22.4969475017253,8.12468288507274,10.7770071894103));
#158038=CARTESIAN_POINT('Ctrl Pts',(22.4658536990385,7.65343574173953,10.4774133220202));
#158039=CARTESIAN_POINT('Ctrl Pts',(22.4535162590206,7.4742482739064,10.342594339537));
#158040=CARTESIAN_POINT('Ctrl Pts',(22.4257158867594,7.10019293920917,10.0120189258201));
#158041=CARTESIAN_POINT('Ctrl Pts',(22.4102301496065,6.91205649731029,9.81016156506494));
#158042=CARTESIAN_POINT('Ctrl Pts',(22.3707596858084,6.48790867091137,9.25619448374488));
#158043=CARTESIAN_POINT('Ctrl Pts',(22.3475308352618,6.28237905215565,8.88448259158381));
#158044=CARTESIAN_POINT('Ctrl Pts',(22.2991991321215,5.97940150598051,8.07147339738871));
#158045=CARTESIAN_POINT('Ctrl Pts',(22.2738562761949,5.8902452696974,7.63252148027423));
#158046=CARTESIAN_POINT('Ctrl Pts',(22.2344286972258,5.85912360595505,6.92661403257636));
#158047=CARTESIAN_POINT('Ctrl Pts',(22.2200564830558,5.87165432098166,6.66495841673331));
#158048=CARTESIAN_POINT('Ctrl Pts',(22.1818399371025,5.96714508365989,5.98621167170793));
#158049=CARTESIAN_POINT('Ctrl Pts',(22.1577019805083,6.08853236073664,5.57748960160242));
#158050=CARTESIAN_POINT('Ctrl Pts',(22.1204989350787,6.37080733470024,4.97416663593735));
#158051=CARTESIAN_POINT('Ctrl Pts',(22.1071797556236,6.49188676873379,4.76403391951975));
#158052=CARTESIAN_POINT('Ctrl Pts',(22.0671855771246,6.90231042658895,4.17413546742915));
#158053=CARTESIAN_POINT('Ctrl Pts',(22.040060765781,7.23814240904191,3.83135520777246));
#158054=CARTESIAN_POINT('Ctrl Pts',(21.9978279990004,7.85152801401269,3.3856746636728));
#158055=CARTESIAN_POINT('Ctrl Pts',(21.9823406925833,8.09524200760288,3.24309973310937));
#158056=CARTESIAN_POINT('Ctrl Pts',(21.9509679532618,8.60524270089143,3.00901993289245));
#158057=CARTESIAN_POINT('Ctrl Pts',(21.935159201254,8.87009885346302,2.91769874568505));
#158058=CARTESIAN_POINT('Ctrl Pts',(21.8880351083181,9.6816113240163,2.7244544592365));
#158059=CARTESIAN_POINT('Ctrl Pts',(21.8580076368599,10.2411734304136,2.70250958797326));
#158060=CARTESIAN_POINT('Ctrl Pts',(21.8117338739207,11.0510219152431,2.82936601039102));
#158061=CARTESIAN_POINT('Ctrl Pts',(21.7966910548133,11.3084374918958,2.89469785587851));
#158062=CARTESIAN_POINT('Ctrl Pts',(21.7658118326499,11.8304223071756,3.08036229437963));
#158063=CARTESIAN_POINT('Ctrl Pts',(21.749931542416,12.0921668051575,3.20465583637065));
#158064=CARTESIAN_POINT('Ctrl Pts',(21.7181459700998,12.5783576346297,3.49937142960535));
#158065=CARTESIAN_POINT('Ctrl Pts',(21.7023349255994,12.8025617882264,3.6674278171189));
#158066=CARTESIAN_POINT('Ctrl Pts',(21.6552251732102,13.4175836166178,4.23068582269741));
#158067=CARTESIAN_POINT('Ctrl Pts',(21.6252026270812,13.7495122674209,4.68135672108846));
#158068=CARTESIAN_POINT('Ctrl Pts',(21.5789375005714,14.0988020859468,5.42264915317206));
#158069=CARTESIAN_POINT('Ctrl Pts',(21.5638953347234,14.1891620494996,5.67239014673362));
#158070=CARTESIAN_POINT('Ctrl Pts',(21.5345432819917,14.3215256214276,6.1823040533484));
#158071=CARTESIAN_POINT('Ctrl Pts',(21.520151853032,14.3638210107639,6.44122196721935));
#158072=CARTESIAN_POINT('Ctrl Pts',(21.4828334512866,14.4105356040433,7.10871520996769));
#158073=CARTESIAN_POINT('Ctrl Pts',(21.4596547429648,14.3805895699774,7.5170209498503));
#158074=CARTESIAN_POINT('Ctrl Pts',(21.4235520815382,14.2420611454006,8.14749736915591));
#158075=CARTESIAN_POINT('Ctrl Pts',(21.4104286147913,14.1715322789947,8.37545902069937));
#158076=CARTESIAN_POINT('Ctrl Pts',(21.3655784812187,13.8699134766247,9.12232448644817));
#158077=CARTESIAN_POINT('Ctrl Pts',(21.3333941001527,13.5546316931928,9.60066090863966));
#158078=CARTESIAN_POINT('Ctrl Pts',(21.2868974827202,12.9628157617956,10.1968584796758));
#158079=CARTESIAN_POINT('Ctrl Pts',(21.2718286027191,12.7525036562347,10.3715618333134));
#158080=CARTESIAN_POINT('Ctrl Pts',(21.2355758124263,12.2187529997089,10.7345835549968));
#158081=CARTESIAN_POINT('Ctrl Pts',(21.2143759062964,11.8843871977691,10.9028804360248));
#158082=CARTESIAN_POINT('Ctrl Pts',(21.1804532628206,11.3089988116208,11.1034041201438));
#158083=CARTESIAN_POINT('Ctrl Pts',(21.167375361928,11.0794965174539,11.1625291571328));
#158084=CARTESIAN_POINT('Ctrl Pts',(21.1407216241085,10.609585791639,11.2426807155862));
#158085=CARTESIAN_POINT('Ctrl Pts',(21.127186528019,10.3699147472305,11.2629817564361));
#158086=CARTESIAN_POINT('Ctrl Pts',(21.1136182667127,10.1298237102038,11.2629999877096));
#158087=CARTESIAN_POINT('Ctrl Pts',(22.2043183294109,10.1294634642048,11.2629999998434));
#158088=CARTESIAN_POINT('Ctrl Pts',(22.1969189590874,9.99730152393924,11.2629988671572));
#158089=CARTESIAN_POINT('Ctrl Pts',(22.189519588764,9.86515952805542,11.2568474502169));
#158090=CARTESIAN_POINT('Ctrl Pts',(22.1821202184405,9.73360519517336,11.2445772820755));
#158091=CARTESIAN_POINT('Ctrl Pts',(22.174718676944,9.60201226073265,11.2323035135386));
#158092=CARTESIAN_POINT('Ctrl Pts',(22.1673171354475,9.4710076462198,11.2139074381013));
#158093=CARTESIAN_POINT('Ctrl Pts',(22.1599155939509,9.34115385194505,11.1894724430227));
#158094=CARTESIAN_POINT('Ctrl Pts',(22.1583218981377,9.31319380492495,11.184211113424));
#158095=CARTESIAN_POINT('Ctrl Pts',(22.1567282023245,9.2852870817884,11.1786699942204));
#158096=CARTESIAN_POINT('Ctrl Pts',(22.1551345065113,9.25743924154365,11.1728502289874));
#158097=CARTESIAN_POINT('Ctrl Pts',(22.1478859733478,9.13078019414404,11.1463804591948));
#158098=CARTESIAN_POINT('Ctrl Pts',(22.1406374401844,9.00530415852921,11.1141348765338));
#158099=CARTESIAN_POINT('Ctrl Pts',(22.1333889070209,8.88154079800544,11.0762442063936));
#158100=CARTESIAN_POINT('Ctrl Pts',(22.1261417954377,8.75780170991764,11.0383609673611));
#158101=CARTESIAN_POINT('Ctrl Pts',(22.1188946838546,8.63577495772857,10.9948349505913));
#158102=CARTESIAN_POINT('Ctrl Pts',(22.1116475722714,8.51597534149411,10.9458468262711));
#158103=CARTESIAN_POINT('Ctrl Pts',(22.1044001904397,8.39617125786865,10.8968568751578));
#158104=CARTESIAN_POINT('Ctrl Pts',(22.0971528086079,8.27859479795234,10.8424045371221));
#158105=CARTESIAN_POINT('Ctrl Pts',(22.0899054267761,8.16374135476003,10.7827188566776));
#158106=CARTESIAN_POINT('Ctrl Pts',(22.0826583545769,8.04889281849421,10.7230357262067));
#158107=CARTESIAN_POINT('Ctrl Pts',(22.0754112823778,7.93676737253154,10.6581198618939));
#158108=CARTESIAN_POINT('Ctrl Pts',(22.0681642101786,7.82783617158518,10.5882464548811));
#158109=CARTESIAN_POINT('Ctrl Pts',(22.0609155607501,7.71888126320527,10.5183578408465));
#158110=CARTESIAN_POINT('Ctrl Pts',(22.0536669113216,7.61312227946226,10.4435097165584));
#158111=CARTESIAN_POINT('Ctrl Pts',(22.0464182618931,7.51100202624902,10.3640210108532));
#158112=CARTESIAN_POINT('Ctrl Pts',(22.0438751284631,7.47517391338621,10.336133004021));
#158113=CARTESIAN_POINT('Ctrl Pts',(22.0413319950331,7.43979341525656,10.3076741642416));
#158114=CARTESIAN_POINT('Ctrl Pts',(22.0387888616031,7.40487871978231,10.2786594637725));
#158115=CARTESIAN_POINT('Ctrl Pts',(22.0315394209714,7.30535110199038,10.1959503357274));
#158116=CARTESIAN_POINT('Ctrl Pts',(22.0242899803397,7.20957401612299,10.1086907026288));
#158117=CARTESIAN_POINT('Ctrl Pts',(22.017040539708,7.11795438636582,10.0172441096141));
#158118=CARTESIAN_POINT('Ctrl Pts',(22.0097925532381,7.02635313454589,9.9258158598272));
#158119=CARTESIAN_POINT('Ctrl Pts',(22.0025445667682,6.93890792009219,9.83020256976117));
#158120=CARTESIAN_POINT('Ctrl Pts',(21.9952965802982,6.85598915380836,9.73080496188683));
#158121=CARTESIAN_POINT('Ctrl Pts',(21.9880483796479,6.77306793724778,9.63140441678055));
#158122=CARTESIAN_POINT('Ctrl Pts',(21.9808001789976,6.6946736606481,9.52821959371692));
#158123=CARTESIAN_POINT('Ctrl Pts',(21.9735519783473,6.62113693951177,9.4216848754125));
#158124=CARTESIAN_POINT('Ctrl Pts',(21.9663041219354,6.54760371085105,9.31515521675584));
#158125=CARTESIAN_POINT('Ctrl Pts',(21.9590562655236,6.47892777135026,9.20527626682615));
#158126=CARTESIAN_POINT('Ctrl Pts',(21.9518084091117,6.41539671901959,9.09251184422229));
#158127=CARTESIAN_POINT('Ctrl Pts',(21.9445590323089,6.35185233970934,8.97972376689994));
#158128=CARTESIAN_POINT('Ctrl Pts',(21.9373096555061,6.2934551725897,8.86404930972835));
#158129=CARTESIAN_POINT('Ctrl Pts',(21.9300602787033,6.24044729171342,8.74597767229963));
#158130=CARTESIAN_POINT('Ctrl Pts',(21.9275212580338,6.22188181928051,8.70462427930307));
#158131=CARTESIAN_POINT('Ctrl Pts',(21.9249822373644,6.20397701830358,8.66297703249349));
#158132=CARTESIAN_POINT('Ctrl Pts',(21.922443216695,6.18674190960378,8.62105756856911));
#158133=CARTESIAN_POINT('Ctrl Pts',(21.9151754459718,6.13740760526893,8.50106600792267));
#158134=CARTESIAN_POINT('Ctrl Pts',(21.9079076752487,6.09354713243275,8.37880167535367));
#158135=CARTESIAN_POINT('Ctrl Pts',(21.9006399045255,6.05534999136786,8.25477914676757));
#158136=CARTESIAN_POINT('Ctrl Pts',(21.8933734613687,6.01715982757829,8.13077927273893));
#158137=CARTESIAN_POINT('Ctrl Pts',(21.8861070182118,5.98463103242785,8.00502217048947));
#158138=CARTESIAN_POINT('Ctrl Pts',(21.878840575055,5.95790341045558,7.87803809376438));
#158139=CARTESIAN_POINT('Ctrl Pts',(21.871573922425,5.93117501799356,7.75105035640947));
#158140=CARTESIAN_POINT('Ctrl Pts',(21.8643072697949,5.91024820677359,7.6228359082289));
#158141=CARTESIAN_POINT('Ctrl Pts',(21.8570406171649,5.89521184619667,7.49393605918256));
#158142=CARTESIAN_POINT('Ctrl Pts',(21.8497743641547,5.8801763125242,7.36504329881022));
#158143=CARTESIAN_POINT('Ctrl Pts',(21.8425081111445,5.8710306198732,7.23546555319564));
#158144=CARTESIAN_POINT('Ctrl Pts',(21.8352418581342,5.86781184389181,7.10574998859196));
#158145=CARTESIAN_POINT('Ctrl Pts',(21.8279743223649,5.8645924996789,6.9760115244532));
#158146=CARTESIAN_POINT('Ctrl Pts',(21.8207067865956,5.86730217015556,6.84613553506541));
#158147=CARTESIAN_POINT('Ctrl Pts',(21.8134392508263,5.87592582273696,6.7166703006725));
#158148=CARTESIAN_POINT('Ctrl Pts',(21.8109920244798,5.878829699714,6.67307495520454));
#158149=CARTESIAN_POINT('Ctrl Pts',(21.8085447981333,5.88240372517832,6.62952616917805));
#158150=CARTESIAN_POINT('Ctrl Pts',(21.8060975717868,5.88664599746917,6.58604479323473));
#158151=CARTESIAN_POINT('Ctrl Pts',(21.7989003324876,5.89912242773205,6.45816701512477));
#158152=CARTESIAN_POINT('Ctrl Pts',(21.7917030931884,5.9173874845122,6.33082262933598));
#158153=CARTESIAN_POINT('Ctrl Pts',(21.7845058538891,5.94137144353383,6.20454529072198));
#158154=CARTESIAN_POINT('Ctrl Pts',(21.777310240048,5.96534998590645,6.07829647117027));
#158155=CARTESIAN_POINT('Ctrl Pts',(21.7701146262068,5.9950447885472,5.95311456770553));
#158156=CARTESIAN_POINT('Ctrl Pts',(21.7629190123656,6.03033483538351,5.82952404843386));
#158157=CARTESIAN_POINT('Ctrl Pts',(21.7557229447161,6.06562710786945,5.705925734636));
#158158=CARTESIAN_POINT('Ctrl Pts',(21.7485268770667,6.10651523595494,5.58391934900157));
#158159=CARTESIAN_POINT('Ctrl Pts',(21.7413308094172,6.15282797750728,5.46401542145645));
#158160=CARTESIAN_POINT('Ctrl Pts',(21.7341348236115,6.199140192326,5.34411285762736));
#158161=CARTESIAN_POINT('Ctrl Pts',(21.7269388378059,6.25087676563492,5.22631303483247));
#158162=CARTESIAN_POINT('Ctrl Pts',(21.7197428520002,6.3078179577087,5.11110737001062));
#158163=CARTESIAN_POINT('Ctrl Pts',(21.7125445442252,6.36477752331817,4.99586453112694));
#158164=CARTESIAN_POINT('Ctrl Pts',(21.7053462364502,6.42694490292231,4.88321784067244));
#158165=CARTESIAN_POINT('Ctrl Pts',(21.6981479286752,6.49405382499079,4.77363522561758));
#158166=CARTESIAN_POINT('Ctrl Pts',(21.6953492614097,6.52014544947959,4.73103003461787));
#158167=CARTESIAN_POINT('Ctrl Pts',(21.6925505941441,6.54698356415018,4.68888773294117));
#158168=CARTESIAN_POINT('Ctrl Pts',(21.6897519268785,6.57455071884714,4.64723468904552));
#158169=CARTESIAN_POINT('Ctrl Pts',(21.6823654767811,6.64730799692895,4.53730088807892));
#158170=CARTESIAN_POINT('Ctrl Pts',(21.6749790266836,6.72517120219222,4.43074005094906));
#158171=CARTESIAN_POINT('Ctrl Pts',(21.6675925765861,6.8078078071312,4.32801010933154));
#158172=CARTESIAN_POINT('Ctrl Pts',(21.6602070407686,6.89043418347741,4.22529288341958));
#158173=CARTESIAN_POINT('Ctrl Pts',(21.652821504951,6.97783258068516,4.12640585384117));
#158174=CARTESIAN_POINT('Ctrl Pts',(21.6454359691335,7.06962978046818,4.03177439543045));
#158175=CARTESIAN_POINT('Ctrl Pts',(21.6380510733541,7.16141902501109,3.93715113787961));
#158176=CARTESIAN_POINT('Ctrl Pts',(21.6306661775747,7.2576060910435,3.84678294446063));
#158177=CARTESIAN_POINT('Ctrl Pts',(21.6232812817953,7.3577801678109,3.76105909719711));
#158178=CARTESIAN_POINT('Ctrl Pts',(21.6158977417591,7.45793585429648,3.67535098739542));
#158179=CARTESIAN_POINT('Ctrl Pts',(21.6085142017228,7.56207684856391,3.59428572780241));
#158180=CARTESIAN_POINT('Ctrl Pts',(21.6011306616865,7.66975832511667,3.51821311783129));
#158181=CARTESIAN_POINT('Ctrl Pts',(21.5937483307954,7.77742216750874,3.4421529656818));
#158182=CARTESIAN_POINT('Ctrl Pts',(21.5863659999042,7.88862507567842,3.3710840148624));
#158183=CARTESIAN_POINT('Ctrl Pts',(21.5789836690131,8.0028919322252,3.30531366337072));
#158184=CARTESIAN_POINT('Ctrl Pts',(21.5771245399989,8.03166832162039,3.28875038944878));
#158185=CARTESIAN_POINT('Ctrl Pts',(21.5752654109847,8.06063888910807,3.27252294045707));
#158186=CARTESIAN_POINT('Ctrl Pts',(21.5734062819705,8.08979577177236,3.25663578296871));
#158187=CARTESIAN_POINT('Ctrl Pts',(21.5663766750943,8.20004171021903,3.19656438896128));
#158188=CARTESIAN_POINT('Ctrl Pts',(21.5593470682181,8.31298831198066,3.14134266250149));
#158189=CARTESIAN_POINT('Ctrl Pts',(21.5523174613419,8.42817722338396,3.0912060926972));
#158190=CARTESIAN_POINT('Ctrl Pts',(21.5452896275042,8.54333708133278,3.04108216855934));
#158191=CARTESIAN_POINT('Ctrl Pts',(21.5382617936664,8.6607377697407,2.99604099920424));
#158192=CARTESIAN_POINT('Ctrl Pts',(21.5312339598286,8.7798993723283,2.95627063890421));
#158193=CARTESIAN_POINT('Ctrl Pts',(21.5242047012697,8.89908513201198,2.9164922161378));
#158194=CARTESIAN_POINT('Ctrl Pts',(21.5171754427108,9.02003215567398,2.88198686387374));
#158195=CARTESIAN_POINT('Ctrl Pts',(21.5101461841518,9.14224366034339,2.85289330739999));
#158196=CARTESIAN_POINT('Ctrl Pts',(21.5031162567188,9.26446679413621,2.82379698250799));
#158197=CARTESIAN_POINT('Ctrl Pts',(21.4960863292857,9.38795427288864,2.80011356232756));
#158198=CARTESIAN_POINT('Ctrl Pts',(21.4890564018526,9.5121981594764,2.78193084010158));
#158199=CARTESIAN_POINT('Ctrl Pts',(21.4820218975376,9.63652293588892,2.76373627989101));
#158200=CARTESIAN_POINT('Ctrl Pts',(21.4749873932226,9.76160472207926,2.75104962078328));
#158201=CARTESIAN_POINT('Ctrl Pts',(21.4679528889076,9.88692926940032,2.74390690413657));
#158202=CARTESIAN_POINT('Ctrl Pts',(21.4643221382925,9.95161359638359,2.74022030139992));
#158203=CARTESIAN_POINT('Ctrl Pts',(21.4606913876774,10.0163625427089,2.73800972683479));
#158204=CARTESIAN_POINT('Ctrl Pts',(21.4570606370622,10.0811053611285,2.737274702854));
#158205=CARTESIAN_POINT('Ctrl Pts',(21.4494491623812,10.216831654508,2.73573380483792));
#158206=CARTESIAN_POINT('Ctrl Pts',(21.4418376877003,10.3526182676046,2.74067973952619));
#158207=CARTESIAN_POINT('Ctrl Pts',(21.4342262130193,10.4878649307102,2.75208950465796));
#158208=CARTESIAN_POINT('Ctrl Pts',(21.4264336112805,10.6263300017054,2.76377078316592));
#158209=CARTESIAN_POINT('Ctrl Pts',(21.4186410095417,10.764228814435,2.78222738393882));
#158210=CARTESIAN_POINT('Ctrl Pts',(21.410848407803,10.9009217006177,2.80737819976378));
#158211=CARTESIAN_POINT('Ctrl Pts',(21.4032429171247,11.0343324030374,2.83192510998959));
#158212=CARTESIAN_POINT('Ctrl Pts',(21.3956374264465,11.1665941568544,2.86284837110384));
#158213=CARTESIAN_POINT('Ctrl Pts',(21.3880319357682,11.2971204731094,2.90002055727401));
#158214=CARTESIAN_POINT('Ctrl Pts',(21.3801457784992,11.4324636220633,2.93856451434043));
#158215=CARTESIAN_POINT('Ctrl Pts',(21.3722596212301,11.5659405054026,2.98382740162559));
#158216=CARTESIAN_POINT('Ctrl Pts',(21.3643734639611,11.6969110187463,3.03560954265189));
#158217=CARTESIAN_POINT('Ctrl Pts',(21.3564873066921,11.8278815320899,3.08739168367819));
#158218=CARTESIAN_POINT('Ctrl Pts',(21.3486011494231,11.956345363596,3.14569299962129));
#158219=CARTESIAN_POINT('Ctrl Pts',(21.340714992154,12.0816810369674,3.21025618294525));
#158220=CARTESIAN_POINT('Ctrl Pts',(21.3336759604758,12.1935532384943,3.26788403351437));
#158221=CARTESIAN_POINT('Ctrl Pts',(21.3266369287976,12.3028932792345,3.33048051016728));
#158222=CARTESIAN_POINT('Ctrl Pts',(21.3195978971194,12.40925055225,3.39779145252306));
#158223=CARTESIAN_POINT('Ctrl Pts',(21.3125590744663,12.5156046669697,3.46510039606998));
#158224=CARTESIAN_POINT('Ctrl Pts',(21.3055202518132,12.6189758680056,3.53712332086819));
#158225=CARTESIAN_POINT('Ctrl Pts',(21.2984814291601,12.7189414344944,3.61356203994173));
#158226=CARTESIAN_POINT('Ctrl Pts',(21.2914389136867,12.8189594465259,3.69004086152499));
#158227=CARTESIAN_POINT('Ctrl Pts',(21.2843963982133,12.9155679496317,3.77093987410838));
#158228=CARTESIAN_POINT('Ctrl Pts',(21.2773538827399,13.0083761165701,3.85591964074671));
#158229=CARTESIAN_POINT('Ctrl Pts',(21.2703094098651,13.1012100786724,3.94092302671816));
#158230=CARTESIAN_POINT('Ctrl Pts',(21.2632649369902,13.1902413235328,4.03000916216276));
#158231=CARTESIAN_POINT('Ctrl Pts',(21.2562204641154,13.2751155328051,4.12280137637754));
#158232=CARTESIAN_POINT('Ctrl Pts',(21.2491695588495,13.3600672417159,4.21567832025411));
#158233=CARTESIAN_POINT('Ctrl Pts',(21.2421186535837,13.4408540813723,4.31226781405213));
#158234=CARTESIAN_POINT('Ctrl Pts',(21.2350677483178,13.5171614727389,4.41215944345081));
#158235=CARTESIAN_POINT('Ctrl Pts',(21.2315016146271,13.5557554332217,4.46268159508693));
#158236=CARTESIAN_POINT('Ctrl Pts',(21.2279354809365,13.5932042061302,4.51404795176234));
#158237=CARTESIAN_POINT('Ctrl Pts',(21.2243693472458,13.6294713302574,4.56620261990112));
#158238=CARTESIAN_POINT('Ctrl Pts',(21.2173459273525,13.7008986134619,4.66892006279847));
#158239=CARTESIAN_POINT('Ctrl Pts',(21.2103225074592,13.7678679518273,4.77488136034603));
#158240=CARTESIAN_POINT('Ctrl Pts',(21.2032990875659,13.8300824556287,4.88366862493296));
#158241=CARTESIAN_POINT('Ctrl Pts',(21.1962814937663,13.8922453510204,4.99236564789809));
#158242=CARTESIAN_POINT('Ctrl Pts',(21.1892638999668,13.9496610740247,5.10388363594717));
#158243=CARTESIAN_POINT('Ctrl Pts',(21.1822463061672,14.0020763560252,5.21777628599693));
#158244=CARTESIAN_POINT('Ctrl Pts',(21.1752329695233,14.0544598407996,5.33159984416752));
#158245=CARTESIAN_POINT('Ctrl Pts',(21.1682196328795,14.1018487643949,5.44779484503741));
#158246=CARTESIAN_POINT('Ctrl Pts',(21.1612062962356,14.1440362326073,5.5658912743158));
#158247=CARTESIAN_POINT('Ctrl Pts',(21.1541426196187,14.1865265118952,5.68483537017137));
#158248=CARTESIAN_POINT('Ctrl Pts',(21.1470789430017,14.223740187332,5.80570794539113));
#158249=CARTESIAN_POINT('Ctrl Pts',(21.1400152663848,14.2555155490246,5.92800900693764));
#158250=CARTESIAN_POINT('Ctrl Pts',(21.1330043158592,14.2870537267815,6.04939716472518));
#158251=CARTESIAN_POINT('Ctrl Pts',(21.1259933653335,14.3132344332075,6.17219216889758));
#158252=CARTESIAN_POINT('Ctrl Pts',(21.1189824148079,14.3339500177816,6.29589130954337));
#158253=CARTESIAN_POINT('Ctrl Pts',(21.1119707905225,14.3546675931453,6.41960233780791));
#158254=CARTESIAN_POINT('Ctrl Pts',(21.104959166237,14.3699189367607,6.54421729408242));
#158255=CARTESIAN_POINT('Ctrl Pts',(21.0979475419516,14.3796478851492,6.66922522109208));
#158256=CARTESIAN_POINT('Ctrl Pts',(21.0909338264986,14.3893797351281,6.79427043083558));
#158257=CARTESIAN_POINT('Ctrl Pts',(21.0839201110456,14.3935858804475,6.91970845912758));
#158258=CARTESIAN_POINT('Ctrl Pts',(21.0769063955927,14.3922622147059,7.04502555802502));
#158259=CARTESIAN_POINT('Ctrl Pts',(21.069804034079,14.3909218192076,7.17192653457186));
#158260=CARTESIAN_POINT('Ctrl Pts',(21.0627016725654,14.3839108701113,7.29870309586766));
#158261=CARTESIAN_POINT('Ctrl Pts',(21.0555993110518,14.37127938786,7.42482540499111));
#158262=CARTESIAN_POINT('Ctrl Pts',(21.0485733953341,14.358783863728,7.54959020502676));
#158263=CARTESIAN_POINT('Ctrl Pts',(21.0415474796164,14.3407883237577,7.67371439178308));
#158264=CARTESIAN_POINT('Ctrl Pts',(21.0345215638987,14.3173929110686,7.79669439901484));
#158265=CARTESIAN_POINT('Ctrl Pts',(21.0273809794871,14.2936156660999,7.92168154059925));
#158266=CARTESIAN_POINT('Ctrl Pts',(21.0202403950756,14.264260841247,8.04548642037499));
#158267=CARTESIAN_POINT('Ctrl Pts',(21.013099810664,14.2294863484673,8.16759622403539));
#158268=CARTESIAN_POINT('Ctrl Pts',(21.0059592262525,14.1947118556876,8.28970602769578));
#158269=CARTESIAN_POINT('Ctrl Pts',(20.9988186418409,14.1545178775712,8.41012037987649));
#158270=CARTESIAN_POINT('Ctrl Pts',(20.9916780574294,14.1091131539846,8.52834817519842));
#158271=CARTESIAN_POINT('Ctrl Pts',(20.9848875792511,14.0659346454851,8.64077920575989));
#158272=CARTESIAN_POINT('Ctrl Pts',(20.9780971010728,14.0179001275206,8.75160660314064));
#158273=CARTESIAN_POINT('Ctrl Pts',(20.9713066228945,13.9651477064359,8.86036976757665));
#158274=CARTESIAN_POINT('Ctrl Pts',(20.9645253559579,13.9124668436842,8.96898539545253));
#158275=CARTESIAN_POINT('Ctrl Pts',(20.9577440890213,13.8550809778343,9.07554198259683));
#158276=CARTESIAN_POINT('Ctrl Pts',(20.9509628220846,13.793177528671,9.17959536747338));
#158277=CARTESIAN_POINT('Ctrl Pts',(20.9441888767195,13.7313409151793,9.28353640840212));
#158278=CARTESIAN_POINT('Ctrl Pts',(20.9374149313544,13.6649966269885,9.38497926183249));
#158279=CARTESIAN_POINT('Ctrl Pts',(20.9306409859893,13.5943792727532,9.48350168617723));
#158280=CARTESIAN_POINT('Ctrl Pts',(20.9238724821202,13.5238186452894,9.58194496766671));
#158281=CARTESIAN_POINT('Ctrl Pts',(20.9171039782511,13.4489920202032,9.67747214528359));
#158282=CARTESIAN_POINT('Ctrl Pts',(20.910335474382,13.370178451617,9.76968810035086));
#158283=CARTESIAN_POINT('Ctrl Pts',(20.903569799622,13.2913978256411,9.8618655108588));
#158284=CARTESIAN_POINT('Ctrl Pts',(20.896804124862,13.2086338378673,9.95073412927473));
#158285=CARTESIAN_POINT('Ctrl Pts',(20.890038450102,13.1222067694605,10.0359306961828));
#158286=CARTESIAN_POINT('Ctrl Pts',(20.8832740089491,13.035795459577,10.1211117289289));
#158287=CARTESIAN_POINT('Ctrl Pts',(20.8765095677961,12.9457226947661,10.2026217459866));
#158288=CARTESIAN_POINT('Ctrl Pts',(20.8697451266432,12.8523461041995,10.2801338528855));
#158289=CARTESIAN_POINT('Ctrl Pts',(20.8629802282965,12.7589632025141,10.3576511986577));
#158290=CARTESIAN_POINT('Ctrl Pts',(20.8562153299499,12.6622763543278,10.4311698294127));
#158291=CARTESIAN_POINT('Ctrl Pts',(20.8494504316032,12.5626761707932,10.5004032227565));
#158292=CARTESIAN_POINT('Ctrl Pts',(20.8426833849945,12.4630443582094,10.5696586018671));
#158293=CARTESIAN_POINT('Ctrl Pts',(20.8359163383857,12.3604977161624,10.6346258000381));
#158294=CARTESIAN_POINT('Ctrl Pts',(20.8291492917769,12.2554550341066,10.6950621365488));
#158295=CARTESIAN_POINT('Ctrl Pts',(20.8223742557459,12.1502883348272,10.7555698264038));
#158296=CARTESIAN_POINT('Ctrl Pts',(20.815599219715,12.0426200781834,10.8115357695555));
#158297=CARTESIAN_POINT('Ctrl Pts',(20.808824183684,11.9328928762342,10.8627636652982));
#158298=CARTESIAN_POINT('Ctrl Pts',(20.8020445915196,11.8230918840095,10.9140260112088));
#158299=CARTESIAN_POINT('Ctrl Pts',(20.7952649993552,11.7112295779413,10.9605438102634));
#158300=CARTESIAN_POINT('Ctrl Pts',(20.7884854071908,11.5977659401151,11.002169927564));
#158301=CARTESIAN_POINT('Ctrl Pts',(20.7816949968921,11.4841212493811,11.0438624672861));
#158302=CARTESIAN_POINT('Ctrl Pts',(20.7749045865934,11.3688705257193,11.0806476224473));
#158303=CARTESIAN_POINT('Ctrl Pts',(20.7681141762946,11.2524863546908,11.1124288014722));
#158304=CARTESIAN_POINT('Ctrl Pts',(20.7650717067341,11.2003399773581,11.1266684814808));
#158305=CARTESIAN_POINT('Ctrl Pts',(20.7620292371736,11.1479661589978,11.1399042936374));
#158306=CARTESIAN_POINT('Ctrl Pts',(20.7589867676131,11.0954077443162,11.1521309263401));
#158307=CARTESIAN_POINT('Ctrl Pts',(20.7486384526106,10.9166414426865,11.193717224612));
#158308=CARTESIAN_POINT('Ctrl Pts',(20.7382901376082,10.7352286283145,11.223745455636));
#158309=CARTESIAN_POINT('Ctrl Pts',(20.7279418226057,10.5523855434177,11.2419732221183));
#158310=CARTESIAN_POINT('Ctrl Pts',(20.7200673248741,10.4132520268103,11.2558435484257));
#158311=CARTESIAN_POINT('Ctrl Pts',(20.7121928271425,10.2732902767665,11.2628818332749));
#158312=CARTESIAN_POINT('Ctrl Pts',(20.7043183294109,10.1330470789259,11.2629985243055));
#158313=CARTESIAN_POINT('Origin',(-23.734,10.1295,7.));
#158314=CARTESIAN_POINT('',(-22.2043183294109,10.1295365081804,11.2629999998437));
#158315=CARTESIAN_POINT('',(-22.6135314280912,10.1295000920819,11.263));
#158316=CARTESIAN_POINT('',(-23.734,10.1295,11.263));
#158317=CARTESIAN_POINT('',(-23.533999981871,12.9193850840203,10.2235360174615));
#158318=CARTESIAN_POINT('Ctrl Pts',(-23.533999981871,12.9193850840203,10.2235360174615));
#158319=CARTESIAN_POINT('Ctrl Pts',(-23.5009788547478,13.3648360859832,
9.83730561563166));
#158320=CARTESIAN_POINT('Ctrl Pts',(-23.4291758459887,14.1588395586771,
8.79502344007021));
#158321=CARTESIAN_POINT('Ctrl Pts',(-23.3185909555933,14.5604905826756,
6.80076298861617));
#158322=CARTESIAN_POINT('Ctrl Pts',(-23.2022453106852,13.9513208636606,
4.74899583476332));
#158323=CARTESIAN_POINT('Ctrl Pts',(-23.0858996657769,12.452270995998,3.22136570469558));
#158324=CARTESIAN_POINT('Ctrl Pts',(-22.9695540208687,10.4123750626855,
2.57356516157568));
#158325=CARTESIAN_POINT('Ctrl Pts',(-22.8532083759605,8.30661439543301,
2.9564333045403));
#158326=CARTESIAN_POINT('Ctrl Pts',(-22.7368627310523,6.62530205950465,
4.28082127060911));
#158327=CARTESIAN_POINT('Ctrl Pts',(-22.6205170861441,5.75991783379543,
6.23835174036327));
#158328=CARTESIAN_POINT('Ctrl Pts',(-22.5041714412359,5.9119701463398,8.37323075593554));
#158329=CARTESIAN_POINT('Ctrl Pts',(-22.3878257963277,7.04603468702391,
10.1883540588533));
#158330=CARTESIAN_POINT('Ctrl Pts',(-22.2878747590527,8.63711446750853,
11.1099400088585));
#158331=CARTESIAN_POINT('Ctrl Pts',(-22.2267056034138,9.72970022779226,
11.2625492465514));
#158332=CARTESIAN_POINT('Ctrl Pts',(-22.2043183294109,10.1295365056039,
11.2626991438894));
#158333=CARTESIAN_POINT('',(-23.534,12.9193325810254,3.77664721604209));
#158334=CARTESIAN_POINT('Origin',(-23.534,10.1295,7.));
#158335=CARTESIAN_POINT('Ctrl Pts',(-23.534,12.9193325810254,3.77664721604209));
#158336=CARTESIAN_POINT('Ctrl Pts',(-23.5168586580598,12.6878910637622,
3.57633309322055));
#158337=CARTESIAN_POINT('Ctrl Pts',(-23.5000542450407,12.4355456847612,
3.40152546405373));
#158338=CARTESIAN_POINT('Ctrl Pts',(-23.4666881757483,11.9114783876185,
3.11643078784149));
#158339=CARTESIAN_POINT('Ctrl Pts',(-23.4502450241458,11.6427807725919,
3.0040609018805));
#158340=CARTESIAN_POINT('Ctrl Pts',(-23.4112911491467,10.984032226903,2.80462331559761));
#158341=CARTESIAN_POINT('Ctrl Pts',(-23.3895178715562,10.5890392288408,
2.74321227034389));
#158342=CARTESIAN_POINT('Ctrl Pts',(-23.3521339750897,9.91912682473691,
2.73350346552896));
#158343=CARTESIAN_POINT('Ctrl Pts',(-23.3367839960271,9.64723138241095,
2.75563212128445));
#158344=CARTESIAN_POINT('Ctrl Pts',(-23.2981650012946,8.97514813831931,
2.87577736451175));
#158345=CARTESIAN_POINT('Ctrl Pts',(-23.275645081719,8.58352778228038,3.00603949148055));
#158346=CARTESIAN_POINT('Ctrl Pts',(-23.2375083553902,7.972206472833,3.31299050935889));
#158347=CARTESIAN_POINT('Ctrl Pts',(-23.2221028377029,7.74019526512778,
3.45893107422773));
#158348=CARTESIAN_POINT('Ctrl Pts',(-23.1745609982425,7.07494413186754,
3.97271405519828));
#158349=CARTESIAN_POINT('Ctrl Pts',(-23.1438258283781,6.6997624203252,4.40545139686439));
#158350=CARTESIAN_POINT('Ctrl Pts',(-23.0985113983711,6.30345136697088,
5.1050910847094));
#158351=CARTESIAN_POINT('Ctrl Pts',(-23.08505282655,6.20404911848136,5.32066599727039));
#158352=CARTESIAN_POINT('Ctrl Pts',(-23.048506070219,5.9817503616778,5.93209744180422));
#158353=CARTESIAN_POINT('Ctrl Pts',(-23.0259779563819,5.89774520043703,
6.33931806570632));
#158354=CARTESIAN_POINT('Ctrl Pts',(-22.9878332334974,5.85828446543936,
7.01713139920122));
#158355=CARTESIAN_POINT('Ctrl Pts',(-22.9727696608249,5.86762836053496,
7.28288238713844));
#158356=CARTESIAN_POINT('Ctrl Pts',(-22.9429381658152,5.93554297343332,
7.80873923758166));
#158357=CARTESIAN_POINT('Ctrl Pts',(-22.9283693246464,5.99388207497819,
8.06770856547383));
#158358=CARTESIAN_POINT('Ctrl Pts',(-22.8916881242178,6.19827579788421,
8.69558095527337));
#158359=CARTESIAN_POINT('Ctrl Pts',(-22.8693946085137,6.3723902759301,9.05271068927232));
#158360=CARTESIAN_POINT('Ctrl Pts',(-22.8320450352526,6.74201792090859,
9.60175977677851));
#158361=CARTESIAN_POINT('Ctrl Pts',(-22.8173301696315,6.91124320118273,
9.80838308598632));
#158362=CARTESIAN_POINT('Ctrl Pts',(-22.7769127817254,7.42355106280853,
10.3263283873352));
#158363=CARTESIAN_POINT('Ctrl Pts',(-22.7508487154543,7.79969368267197,
10.599803533184));
#158364=CARTESIAN_POINT('Ctrl Pts',(-22.6994967655324,8.61502871430095,
11.010342875459));
#158365=CARTESIAN_POINT('Ctrl Pts',(-22.6749853207843,9.04737808066313,
11.1479500333799));
#158366=CARTESIAN_POINT('Ctrl Pts',(-22.6376180791365,9.70387868628257,
11.2470462297682));
#158367=CARTESIAN_POINT('Ctrl Pts',(-22.625542538647,9.91656672784588,11.2630000045994));
#158368=CARTESIAN_POINT('Ctrl Pts',(-22.6135314280911,10.1295000920819,
11.263));
#158369=CARTESIAN_POINT('Origin',(-23.734,10.1295,7.));
#158370=CARTESIAN_POINT('',(-20.7043183294109,10.1259540174844,11.2629985252177));
#158371=CARTESIAN_POINT('',(-21.113681670589,10.1291791134783,11.262999987923));
#158372=CARTESIAN_POINT('',(-23.734,10.1295,11.263));
#158373=CARTESIAN_POINT('Ctrl Pts',(-22.2043183294109,10.1295365081804,
11.2629999998437));
#158374=CARTESIAN_POINT('Ctrl Pts',(-22.1969189537551,10.2616985400649,
11.2629988680127));
#158375=CARTESIAN_POINT('Ctrl Pts',(-22.1895195780993,10.3938406290833,
11.2568474434062));
#158376=CARTESIAN_POINT('Ctrl Pts',(-22.1821202024435,10.5253950557853,
11.2445772586684));
#158377=CARTESIAN_POINT('Ctrl Pts',(-22.1747186558373,10.6569880800865,
11.2323034739021));
#158378=CARTESIAN_POINT('Ctrl Pts',(-22.1673171092311,10.7879927851824,
11.2139073736701));
#158379=CARTESIAN_POINT('Ctrl Pts',(-22.159915562625,10.917846669891,11.1894723448272));
#158380=CARTESIAN_POINT('Ctrl Pts',(-22.1583218772537,10.9458065338851,
11.184211046063));
#158381=CARTESIAN_POINT('Ctrl Pts',(-22.1567281918825,10.9737130747608,
11.1786699613311));
#158382=CARTESIAN_POINT('Ctrl Pts',(-22.1551345065113,11.0015607336212,
11.1728502341776));
#158383=CARTESIAN_POINT('Ctrl Pts',(-22.1478859815791,11.1282196420853,
11.146380494207));
#158384=CARTESIAN_POINT('Ctrl Pts',(-22.1406374566469,11.2536955421307,
11.1141349538837));
#158385=CARTESIAN_POINT('Ctrl Pts',(-22.1333889317147,11.3774587715464,
11.076244338177));
#158386=CARTESIAN_POINT('Ctrl Pts',(-22.1261418283556,11.5011977286471,
11.0383611535383));
#158387=CARTESIAN_POINT('Ctrl Pts',(-22.1188947249966,11.6232243543046,
10.9948352032451));
#158388=CARTESIAN_POINT('Ctrl Pts',(-22.1116476216375,11.7430238495479,
10.9458471570678));
#158389=CARTESIAN_POINT('Ctrl Pts',(-22.1044002479377,11.8628278137052,
10.8968572834758));
#158390=CARTESIAN_POINT('Ctrl Pts',(-22.0971528742379,11.980404159636,10.8424050344898));
#158391=CARTESIAN_POINT('Ctrl Pts',(-22.0899055005381,12.0952574954049,
10.7827194542101));
#158392=CARTESIAN_POINT('Ctrl Pts',(-22.0826584363958,12.2101059254377,
10.7230364232835));
#158393=CARTESIAN_POINT('Ctrl Pts',(-22.0754113722534,12.3222312716713,
10.6581206695218));
#158394=CARTESIAN_POINT('Ctrl Pts',(-22.068164308111,12.4311623804912,10.5882473836445));
#158395=CARTESIAN_POINT('Ctrl Pts',(-22.0609156665626,12.5401171994071,
10.518358889051));
#158396=CARTESIAN_POINT('Ctrl Pts',(-22.0536670250143,12.6458761011336,
10.44351089455));
#158397=CARTESIAN_POINT('Ctrl Pts',(-22.0464183834659,12.7479962808951,
10.3640223285434));
#158398=CARTESIAN_POINT('Ctrl Pts',(-22.0438752095116,12.7838249778501,
10.3361338960173));
#158399=CARTESIAN_POINT('Ctrl Pts',(-22.0413320355574,12.8192060458866,
10.3076746123286));
#158400=CARTESIAN_POINT('Ctrl Pts',(-22.0387888616031,12.8541212962082,
10.2786594504841));
#158401=CARTESIAN_POINT('Ctrl Pts',(-22.031539428324,12.9536488087519,10.1959504090815));
#158402=CARTESIAN_POINT('Ctrl Pts',(-22.0242899950448,13.0494257988114,
10.1086908709218));
#158403=CARTESIAN_POINT('Ctrl Pts',(-22.0170405617656,13.1410453426988,
10.0172443800378));
#158404=CARTESIAN_POINT('Ctrl Pts',(-22.0097925827507,13.2326465073522,
9.92581623367245));
#158405=CARTESIAN_POINT('Ctrl Pts',(-22.0025446037358,13.3200916446912,
9.83020305433749));
#158406=CARTESIAN_POINT('Ctrl Pts',(-21.995296624721,13.403010344373,9.73080556343414));
#158407=CARTESIAN_POINT('Ctrl Pts',(-21.9880484316003,13.4859314934781,
9.63140513632307));
#158408=CARTESIAN_POINT('Ctrl Pts',(-21.9808002384797,13.5643257132272,
9.52822043757356));
#158409=CARTESIAN_POINT('Ctrl Pts',(-21.9735520453591,13.6378623885564,
9.42168584885883));
#158410=CARTESIAN_POINT('Ctrl Pts',(-21.9663041964995,13.7113955711792,
9.31515632012311));
#158411=CARTESIAN_POINT('Ctrl Pts',(-21.9590563476399,13.7800714757143,
9.20527750541175));
#158412=CARTESIAN_POINT('Ctrl Pts',(-21.9518084987802,13.8436025045761,
9.09251322230027));
#158413=CARTESIAN_POINT('Ctrl Pts',(-21.944559129499,13.9071468606959,8.97972528399669));
#158414=CARTESIAN_POINT('Ctrl Pts',(-21.9373097602177,13.9655440160801,
8.86405097009525));
#158415=CARTESIAN_POINT('Ctrl Pts',(-21.9300603909365,14.0185518970943,
8.74597947917691));
#158416=CARTESIAN_POINT('Ctrl Pts',(-21.927521332856,14.0371176623904,8.70462548526887));
#158417=CARTESIAN_POINT('Ctrl Pts',(-21.9249822747754,14.0550227368446,
8.66297762867509));
#158418=CARTESIAN_POINT('Ctrl Pts',(-21.9224432166949,14.072258099233,8.62105754707614));
#158419=CARTESIAN_POINT('Ctrl Pts',(-21.9151753922206,14.1215927676882,
8.50106509895149));
#158420=CARTESIAN_POINT('Ctrl Pts',(-21.9079075677462,14.1654535201482,
8.37879985409838));
#158421=CARTESIAN_POINT('Ctrl Pts',(-21.9006397432719,14.2036508556539,
8.25477639656434));
#158422=CARTESIAN_POINT('Ctrl Pts',(-21.8933732460253,14.2418412156796,
8.13077558781263));
#158423=CARTESIAN_POINT('Ctrl Pts',(-21.8861067487787,14.2743701213767,
8.0050175340044));
#158424=CARTESIAN_POINT('Ctrl Pts',(-21.8788402515321,14.3010977675838,
7.87803249683022));
#158425=CARTESIAN_POINT('Ctrl Pts',(-21.8715735448853,14.3278261840071,
7.75104380030113));
#158426=CARTESIAN_POINT('Ctrl Pts',(-21.8643068382385,14.3487529329938,
7.6228283840705));
#158427=CARTESIAN_POINT('Ctrl Pts',(-21.8570401315917,14.3637891445478,
7.49392756590881));
#158428=CARTESIAN_POINT('Ctrl Pts',(-21.8497738247676,14.3788245287919,
7.36503384002021));
#158429=CARTESIAN_POINT('Ctrl Pts',(-21.8425075179435,14.3879699855593,
7.23545512785121));
#158430=CARTESIAN_POINT('Ctrl Pts',(-21.8352412111193,14.3911884386049,
7.10573860345731));
#158431=CARTESIAN_POINT('Ctrl Pts',(-21.8279736222961,14.3944074594842,
6.97599919309588));
#158432=CARTESIAN_POINT('Ctrl Pts',(-21.8207060334729,14.3916973798453,
6.84612226427044));
#158433=CARTESIAN_POINT('Ctrl Pts',(-21.8134384446498,14.3830732316722,
6.71665610505596));
#158434=CARTESIAN_POINT('Ctrl Pts',(-21.8109914870288,14.3801695278977,
6.67306555354588));
#158435=CARTESIAN_POINT('Ctrl Pts',(-21.8085445294078,14.3765958228007,
6.62952155223097));
#158436=CARTESIAN_POINT('Ctrl Pts',(-21.8060975717868,14.3723540173125,
6.58604494473972));
#158437=CARTESIAN_POINT('Ctrl Pts',(-21.7989004737786,14.35987783482,6.45816965891825));
#158438=CARTESIAN_POINT('Ctrl Pts',(-21.7917033757704,14.3416132490332,
6.33082772123226));
#158439=CARTESIAN_POINT('Ctrl Pts',(-21.7845062777622,14.3176299764922,
6.20455276730157));
#158440=CARTESIAN_POINT('Ctrl Pts',(-21.7773108057981,14.2936521225045,
6.07830634273716));
#158441=CARTESIAN_POINT('Ctrl Pts',(-21.770115333834,14.2639582246201,5.95312677071234));
#158442=CARTESIAN_POINT('Ctrl Pts',(-21.7629198618699,14.2286692912606,
5.82953850059646));
#158443=CARTESIAN_POINT('Ctrl Pts',(-21.7557239357197,14.1933781304247,
5.70594242945247));
#158444=CARTESIAN_POINT('Ctrl Pts',(-21.7485280095695,14.1524913221394,
5.5839382043744));
#158445=CARTESIAN_POINT('Ctrl Pts',(-21.7413320834193,14.1061801009768,
5.46403633685718));
#158446=CARTESIAN_POINT('Ctrl Pts',(-21.7341362386062,14.0598694032798,
5.34413582461646));
#158447=CARTESIAN_POINT('Ctrl Pts',(-21.7269403937931,14.0081345469274,
5.22633795320274));
#158448=CARTESIAN_POINT('Ctrl Pts',(-21.7197445489799,13.951195264075,5.11113412108044));
#158449=CARTESIAN_POINT('Ctrl Pts',(-21.7125463803664,13.8942375934544,
4.9958930854447));
#158450=CARTESIAN_POINT('Ctrl Pts',(-21.7053482117529,13.8320722985288,
4.8832480808549));
#158451=CARTESIAN_POINT('Ctrl Pts',(-21.6981500431394,13.7649656431987,
4.77366701566866));
#158452=CARTESIAN_POINT('Ctrl Pts',(-21.6953506710525,13.7388678247307,
4.73105087375697));
#158453=CARTESIAN_POINT('Ctrl Pts',(-21.6925512989656,13.7120231386475,
4.68889785170956));
#158454=CARTESIAN_POINT('Ctrl Pts',(-21.6897519268786,13.6844490489701,
4.64723433822518));
#158455=CARTESIAN_POINT('Ctrl Pts',(-21.6823651612314,13.6116886826953,
4.53729589467605));
#158456=CARTESIAN_POINT('Ctrl Pts',(-21.6749783955841,13.5338219832499,
4.43073073882055));
#158457=CARTESIAN_POINT('Ctrl Pts',(-21.6675916299368,13.4511815146991,
4.32799683478733));
#158458=CARTESIAN_POINT('Ctrl Pts',(-21.6602057767909,13.3685512548839,
4.2252756216705));
#158459=CARTESIAN_POINT('Ctrl Pts',(-21.652819923645,13.281148602485,4.12638496293451));
#158460=CARTESIAN_POINT('Ctrl Pts',(-21.645434070499,13.1893468117984,4.03175026516851));
#158461=CARTESIAN_POINT('Ctrl Pts',(-21.6380488592528,13.0975529995455,
3.93712379204228));
#158462=CARTESIAN_POINT('Ctrl Pts',(-21.6306636480065,13.0013610322878,
3.84675277061771));
#158463=CARTESIAN_POINT('Ctrl Pts',(-21.6232784367602,12.9011817562969,
3.76102651418525));
#158464=CARTESIAN_POINT('Ctrl Pts',(-21.6158945838923,12.8010209065034,
3.67531602557404));
#158465=CARTESIAN_POINT('Ctrl Pts',(-21.6085107310244,12.6968744537646,
3.59424880257396));
#158466=CARTESIAN_POINT('Ctrl Pts',(-21.6011268781565,12.5891872591908,
3.51817467598181));
#158467=CARTESIAN_POINT('Ctrl Pts',(-21.5937442414511,12.4815178013097,
3.44211307923043));
#158468=CARTESIAN_POINT('Ctrl Pts',(-21.5863616047457,12.3703090248018,
3.37104312100045));
#158469=CARTESIAN_POINT('Ctrl Pts',(-21.5789789680403,12.2560360828037,
3.30527223079506));
#158470=CARTESIAN_POINT('Ctrl Pts',(-21.577121406017,12.2272836077984,3.2887234674252));
#158471=CARTESIAN_POINT('Ctrl Pts',(-21.5752638439937,12.1983372842333,
3.27250996499309));
#158472=CARTESIAN_POINT('Ctrl Pts',(-21.5734062819704,12.1692049547297,
3.25663617882909));
#158473=CARTESIAN_POINT('Ctrl Pts',(-21.5663770387532,12.0589646359696,
3.19656781915905));
#158474=CARTESIAN_POINT('Ctrl Pts',(-21.5593477955361,11.9460238764199,
3.14134860569491));
#158475=CARTESIAN_POINT('Ctrl Pts',(-21.5523185523189,11.8308409812737,
3.09121401641908));
#158476=CARTESIAN_POINT('Ctrl Pts',(-21.5452910829351,11.7156871525937,
3.04109207863409));
#158477=CARTESIAN_POINT('Ctrl Pts',(-21.5382636135512,11.598292668025,2.99605236218513));
#158478=CARTESIAN_POINT('Ctrl Pts',(-21.5312361441674,11.4791373964743,
2.95628291073201));
#158479=CARTESIAN_POINT('Ctrl Pts',(-21.5242072492004,11.3599579532428,
2.91650539170054));
#158480=CARTESIAN_POINT('Ctrl Pts',(-21.5171783542334,11.2390173728664,
2.88200040031871));
#158481=CARTESIAN_POINT('Ctrl Pts',(-21.5101494592664,11.1168123916017,
2.85290665147386));
#158482=CARTESIAN_POINT('Ctrl Pts',(-21.5031198947892,10.9945957701737,
2.82381013141641));
#158483=CARTESIAN_POINT('Ctrl Pts',(-21.496090330312,10.8711148837365,2.80012596375325));
#158484=CARTESIAN_POINT('Ctrl Pts',(-21.4890607658348,10.7468776224925,
2.78194193126202));
#158485=CARTESIAN_POINT('Ctrl Pts',(-21.4820266213085,10.6225594155855,
2.76374605112903));
#158486=CARTESIAN_POINT('Ctrl Pts',(-21.4749924767822,10.4974842312982,
2.75105751390997));
#158487=CARTESIAN_POINT('Ctrl Pts',(-21.4679583322559,10.3721662707993,
2.7439123504072));
#158488=CARTESIAN_POINT('Ctrl Pts',(-21.4643257671913,10.3074497095221,
2.74022245304675));
#158489=CARTESIAN_POINT('Ctrl Pts',(-21.4606932021268,10.2426684536507,
2.73801005930991));
#158490=CARTESIAN_POINT('Ctrl Pts',(-21.4570606370622,10.1778933606384,
2.73727468834243));
#158491=CARTESIAN_POINT('Ctrl Pts',(-21.4494486360556,10.0421578502062,
2.73573372639261));
#158492=CARTESIAN_POINT('Ctrl Pts',(-21.4418366350489,9.90636208137426,
2.74068047835051));
#158493=CARTESIAN_POINT('Ctrl Pts',(-21.4342246340423,9.77110640803279,
2.75209192269456));
#158494=CARTESIAN_POINT('Ctrl Pts',(-21.4264321638849,9.63264402511851,
2.76377391530407));
#158495=CARTESIAN_POINT('Ctrl Pts',(-21.4186396937276,9.49474795528324,
2.78223096696343));
#158496=CARTESIAN_POINT('Ctrl Pts',(-21.4108472235702,9.35805779034524,
2.80738197337714));
#158497=CARTESIAN_POINT('Ctrl Pts',(-21.4032412105133,9.22463832793057,
2.83193117014216));
#158498=CARTESIAN_POINT('Ctrl Pts',(-21.3956351974563,9.09236799004524,
2.86285756196605));
#158499=CARTESIAN_POINT('Ctrl Pts',(-21.3880291843993,8.96183334801938,
2.90003370869316));
#158500=CARTESIAN_POINT('Ctrl Pts',(-21.3801434856918,8.82649873181441,
2.93857688367882));
#158501=CARTESIAN_POINT('Ctrl Pts',(-21.3722577869842,8.69303018501617,
2.98383817560741));
#158502=CARTESIAN_POINT('Ctrl Pts',(-21.3643720882767,8.56206766416862,
3.03561797090767));
#158503=CARTESIAN_POINT('Ctrl Pts',(-21.3564863895691,8.43110514332108,
3.08739776620794));
#158504=CARTESIAN_POINT('Ctrl Pts',(-21.3486006908616,8.30264895994336,
3.14569598622589));
#158505=CARTESIAN_POINT('Ctrl Pts',(-21.340714992154,8.17732045741597,3.2102554131556));
#158506=CARTESIAN_POINT('Ctrl Pts',(-21.3336761719785,8.06545151277584,
3.26788153021242));
#158507=CARTESIAN_POINT('Ctrl Pts',(-21.3266373518029,7.95611455042713,
3.33047599778825));
#158508=CARTESIAN_POINT('Ctrl Pts',(-21.3195985316273,7.84976015631307,
3.39778467535514));
#158509=CARTESIAN_POINT('Ctrl Pts',(-21.3125599213837,7.74340893420629,
3.46509134544864));
#158510=CARTESIAN_POINT('Ctrl Pts',(-21.3055213111402,7.6400404255637,3.53711173986184));
#158511=CARTESIAN_POINT('Ctrl Pts',(-21.2984827008966,7.54007733081936,
3.61354769111783));
#158512=CARTESIAN_POINT('Ctrl Pts',(-21.2914403979205,7.44006179149318,
3.69002374368832));
#158513=CARTESIAN_POINT('Ctrl Pts',(-21.2843980949443,7.34345554026389,
3.77091974958848));
#158514=CARTESIAN_POINT('Ctrl Pts',(-21.2773557919682,7.25064938419331,
3.85589629117145));
#158515=CARTESIAN_POINT('Ctrl Pts',(-21.270311531557,7.15781743229572,3.94089645231006));
#158516=CARTESIAN_POINT('Ctrl Pts',(-21.2632672711458,7.06878795662045,
4.02997914451082));
#158517=CARTESIAN_POINT('Ctrl Pts',(-21.2562230107345,6.98391525521804,
4.12276771646865));
#158518=CARTESIAN_POINT('Ctrl Pts',(-21.2491723165041,6.89896503600872,
4.21564103613083));
#158519=CARTESIAN_POINT('Ctrl Pts',(-21.2421216222736,6.8181794261953,4.31222670801673));
#158520=CARTESIAN_POINT('Ctrl Pts',(-21.2350709280432,6.74187298426385,
4.41211433748425));
#158521=CARTESIAN_POINT('Ctrl Pts',(-21.2315037344441,6.70326687792428,
4.46265099399217));
#158522=CARTESIAN_POINT('Ctrl Pts',(-21.2279365408449,6.6658066369646,4.51403236253905));
#158523=CARTESIAN_POINT('Ctrl Pts',(-21.2243693472458,6.62952875518707,
4.56620249702597));
#158524=CARTESIAN_POINT('Ctrl Pts',(-21.2173459196766,6.55810143621733,
4.66891998366267));
#158525=CARTESIAN_POINT('Ctrl Pts',(-21.2103224921073,6.49113206267362,
4.77488133278218));
#158526=CARTESIAN_POINT('Ctrl Pts',(-21.203299064538,6.42891752586231,4.88366865729751));
#158527=CARTESIAN_POINT('Ctrl Pts',(-21.1962814635001,6.3667546013078,4.99236573346224));
#158528=CARTESIAN_POINT('Ctrl Pts',(-21.1892638624622,6.30933885072374,
5.10388378270884));
#158529=CARTESIAN_POINT('Ctrl Pts',(-21.1822462614242,6.25692354442136,
5.21777650231572));
#158530=CARTESIAN_POINT('Ctrl Pts',(-21.1752329179883,6.20454003866059,
5.33160012282876));
#158531=CARTESIAN_POINT('Ctrl Pts',(-21.1682195745524,6.15715109672532,
5.44779519409355));
#158532=CARTESIAN_POINT('Ctrl Pts',(-21.1612062311164,6.11496361461179,
5.5658917019994));
#158533=CARTESIAN_POINT('Ctrl Pts',(-21.1541425572128,6.07247337879379,
5.6848357161669));
#158534=CARTESIAN_POINT('Ctrl Pts',(-21.1470788833092,6.03525973704695,
5.80570821283149));
#158535=CARTESIAN_POINT('Ctrl Pts',(-21.1400152094056,6.00348440058743,
5.92800920087711));
#158536=CARTESIAN_POINT('Ctrl Pts',(-21.133004253243,5.97194621040375,6.04939742993803));
#158537=CARTESIAN_POINT('Ctrl Pts',(-21.1259932970804,5.94576549596376,
6.17219251371173));
#158538=CARTESIAN_POINT('Ctrl Pts',(-21.1189823409179,5.925049909777,6.29589174211361));
#158539=CARTESIAN_POINT('Ctrl Pts',(-21.1119707114441,5.90433233412748,
6.41960285021839));
#158540=CARTESIAN_POINT('Ctrl Pts',(-21.1049590819704,5.88908099593137,
6.54421789437491));
#158541=CARTESIAN_POINT('Ctrl Pts',(-21.0979474524966,5.87935206069904,
6.66922591689215));
#158542=CARTESIAN_POINT('Ctrl Pts',(-21.0909337323132,5.86962022451783,
6.79427121398003));
#158543=CARTESIAN_POINT('Ctrl Pts',(-21.0839200121298,5.86541410001686,
6.91970933719594));
#158544=CARTESIAN_POINT('Ctrl Pts',(-21.0769062919464,5.86673779564441,
7.04502653792429));
#158545=CARTESIAN_POINT('Ctrl Pts',(-21.06980393907,5.8680782188723,7.17192737767607));
#158546=CARTESIAN_POINT('Ctrl Pts',(-21.0627015861936,5.87508918354248,
7.29870380973344));
#158547=CARTESIAN_POINT('Ctrl Pts',(-21.0555992333171,5.88772067164072,
7.42482599909129));
#158548=CARTESIAN_POINT('Ctrl Pts',(-21.0485733140547,5.90021622305687,
7.54959089532375));
#158549=CARTESIAN_POINT('Ctrl Pts',(-21.0415473947922,5.9182117997394,7.67371518534136));
#158550=CARTESIAN_POINT('Ctrl Pts',(-21.0345214755298,5.9416072606581,7.79669530171039));
#158551=CARTESIAN_POINT('Ctrl Pts',(-21.0273809058464,5.96538449360439,
7.92168223335618));
#158552=CARTESIAN_POINT('Ctrl Pts',(-21.020240336163,5.99473928967706,8.04548691534146));
#158553=CARTESIAN_POINT('Ctrl Pts',(-21.0130997664796,6.02951374026827,
8.16759653562821));
#158554=CARTESIAN_POINT('Ctrl Pts',(-21.0059591967962,6.06428819085948,
8.28970615591497));
#158555=CARTESIAN_POINT('Ctrl Pts',(-20.9988186271128,6.10448211338605,
8.41012033914232));
#158556=CARTESIAN_POINT('Ctrl Pts',(-20.9916780574294,6.14988677165161,
8.52834798156522));
#158557=CARTESIAN_POINT('Ctrl Pts',(-20.9848875394138,6.19306556040558,
8.6407797582169));
#158558=CARTESIAN_POINT('Ctrl Pts',(-20.9780970213983,6.24110041539954,
8.75160786112374));
#158559=CARTESIAN_POINT('Ctrl Pts',(-20.9713065033827,6.29385322449215,
8.86037168693147));
#158560=CARTESIAN_POINT('Ctrl Pts',(-20.964525196406,6.34653447672102,8.96898797939648));
#158561=CARTESIAN_POINT('Ctrl Pts',(-20.9577438894292,6.40392078324138,
9.07554518694513));
#158562=CARTESIAN_POINT('Ctrl Pts',(-20.9509625824525,6.46582471863268,
9.17959914495719));
#158563=CARTESIAN_POINT('Ctrl Pts',(-20.9441885968762,6.52766181978393,
9.28354076169135));
#158564=CARTESIAN_POINT('Ctrl Pts',(-20.9374146112999,6.59400664137681,
9.38498414360832));
#158565=CARTESIAN_POINT('Ctrl Pts',(-20.9306406257236,6.66462456931131,
9.48350704645866));
#158566=CARTESIAN_POINT('Ctrl Pts',(-20.923872081502,6.73518577182298,9.58195080859381));
#158567=CARTESIAN_POINT('Ctrl Pts',(-20.9171035372804,6.81001301240761,
9.67747841681211));
#158568=CARTESIAN_POINT('Ctrl Pts',(-20.9103349930588,6.88882723169973,
9.76969475011184));
#158569=CARTESIAN_POINT('Ctrl Pts',(-20.9035692778455,6.96760850947957,
9.8618725402971));
#158570=CARTESIAN_POINT('Ctrl Pts',(-20.8968035626323,7.05037318437453,
9.9507414859558));
#158571=CARTESIAN_POINT('Ctrl Pts',(-20.890037847419,7.13680097017415,10.0359383256054));
#158572=CARTESIAN_POINT('Ctrl Pts',(-20.8832733657405,7.2232129983373,10.1211196320463));
#158573=CARTESIAN_POINT('Ctrl Pts',(-20.8765088840621,7.31328651177657,
10.2026298682361));
#158574=CARTESIAN_POINT('Ctrl Pts',(-20.8697444023836,7.40666387645209,
10.28014213782));
#158575=CARTESIAN_POINT('Ctrl Pts',(-20.8629794634639,7.50004755291707,
10.3576596468014));
#158576=CARTESIAN_POINT('Ctrl Pts',(-20.8562145245441,7.59673520141363,
10.4311783842624));
#158577=CARTESIAN_POINT('Ctrl Pts',(-20.8494495856244,7.6963362060632,10.5004118260392));
#158578=CARTESIAN_POINT('Ctrl Pts',(-20.8426824984199,7.79596884016584,
10.5696672536977));
#158579=CARTESIAN_POINT('Ctrl Pts',(-20.8359154112155,7.8985163245618,10.6346344420979));
#158580=CARTESIAN_POINT('Ctrl Pts',(-20.829148324011,8.00355986516484,10.6950707088088));
#158581=CARTESIAN_POINT('Ctrl Pts',(-20.8223732475449,8.10872742076868,
10.7555783269196));
#158582=CARTESIAN_POINT('Ctrl Pts',(-20.8155981710788,8.21639654982388,
10.8115441384382));
#158583=CARTESIAN_POINT('Ctrl Pts',(-20.8088230946128,8.3261246357037,10.8627718409776));
#158584=CARTESIAN_POINT('Ctrl Pts',(-20.8020434620293,8.43592651175376,
10.9140339932283));
#158585=CARTESIAN_POINT('Ctrl Pts',(-20.7952638294458,8.54778971316061,
10.9605515370318));
#158586=CARTESIAN_POINT('Ctrl Pts',(-20.7884841968622,8.66125425324206,
11.002177335792));
#158587=CARTESIAN_POINT('Ctrl Pts',(-20.7816937465263,8.77489984020051,
11.0438695537248));
#158588=CARTESIAN_POINT('Ctrl Pts',(-20.7749032961903,8.89015146681934,
11.0806543242509));
#158589=CARTESIAN_POINT('Ctrl Pts',(-20.7681128458544,9.00653654290877,
11.1124350540814));
#158590=CARTESIAN_POINT('Ctrl Pts',(-20.7650708197739,9.05867541725731,
11.1266723732895));
#158591=CARTESIAN_POINT('Ctrl Pts',(-20.7620287936935,9.11104166406988,
11.1399061162083));
#158592=CARTESIAN_POINT('Ctrl Pts',(-20.7589867676131,9.16359245771118,
11.1521309733376));
#158593=CARTESIAN_POINT('Ctrl Pts',(-20.7486393029828,9.34234420543419,
11.1937138767748));
#158594=CARTESIAN_POINT('Ctrl Pts',(-20.7382918383526,9.5237420713755,11.2237406026673));
#158595=CARTESIAN_POINT('Ctrl Pts',(-20.7279443737223,9.70657007694164,
11.2419687976436));
#158596=CARTESIAN_POINT('Ctrl Pts',(-20.7200690256185,9.84571857741016,
11.2558420879492));
#158597=CARTESIAN_POINT('Ctrl Pts',(-20.7121936775147,9.9856955507432,11.2628818575557));
#158598=CARTESIAN_POINT('Ctrl Pts',(-20.7043183294109,10.1259540174844,
11.2629985252177));
#158599=CARTESIAN_POINT('Ctrl Pts',(-22.6135314280912,10.1295000920819,
11.263));
#158600=CARTESIAN_POINT('Ctrl Pts',(-22.6114426391579,10.1665302112095,
11.2629999992001));
#158601=CARTESIAN_POINT('Ctrl Pts',(-22.6093563312962,10.2035677796465,
11.262517511459));
#158602=CARTESIAN_POINT('Ctrl Pts',(-22.5828596258304,10.6748181369334,
11.250231487439));
#158603=CARTESIAN_POINT('Ctrl Pts',(-22.5592251208326,11.1047589224831,
11.172614884571));
#158604=CARTESIAN_POINT('Ctrl Pts',(-22.5159786266063,11.83186799329,10.9226282195187));
#158605=CARTESIAN_POINT('Ctrl Pts',(-22.4969476089091,12.1343159013056,
10.777008501496));
#158606=CARTESIAN_POINT('Ctrl Pts',(-22.4658534516122,12.6055680940911,
10.4774105216325));
#158607=CARTESIAN_POINT('Ctrl Pts',(-22.4535160694584,12.7847545671071,
10.3425920108082));
#158608=CARTESIAN_POINT('Ctrl Pts',(-22.4257157609656,13.1588088195395,
10.0120171476607));
#158609=CARTESIAN_POINT('Ctrl Pts',(-22.4102300281437,13.3469450757265,
9.81015975406352));
#158610=CARTESIAN_POINT('Ctrl Pts',(-22.3707596136098,13.7710920754039,
9.25619313536883));
#158611=CARTESIAN_POINT('Ctrl Pts',(-22.3475308067559,13.9766212163167,
8.88448187132161));
#158612=CARTESIAN_POINT('Ctrl Pts',(-22.2991991860079,14.2795982494886,
8.07147405339804));
#158613=CARTESIAN_POINT('Ctrl Pts',(-22.2738563707513,14.3687544511833,
7.63252285753962));
#158614=CARTESIAN_POINT('Ctrl Pts',(-22.2344289353595,14.3998763445003,
6.92661806501799));
#158615=CARTESIAN_POINT('Ctrl Pts',(-22.2200568265937,14.3873460295288,
6.66496438588235));
#158616=CARTESIAN_POINT('Ctrl Pts',(-22.1818402111224,14.2918563360692,
5.98621612201307));
#158617=CARTESIAN_POINT('Ctrl Pts',(-22.1577020672557,14.1704683909691,
5.57749075443616));
#158618=CARTESIAN_POINT('Ctrl Pts',(-22.1204988010786,13.8881914365572,
4.97416426877736));
#158619=CARTESIAN_POINT('Ctrl Pts',(-22.1071795825062,13.7671114862297,
4.76403100142559));
#158620=CARTESIAN_POINT('Ctrl Pts',(-22.0671856153995,13.356689442883,4.174136086842));
#158621=CARTESIAN_POINT('Ctrl Pts',(-22.040061063534,13.0208609312589,3.83135894128661));
#158622=CARTESIAN_POINT('Ctrl Pts',(-21.997829069187,12.4074877547101,3.38568534891367));
#158623=CARTESIAN_POINT('Ctrl Pts',(-21.982342286845,12.1637828884393,3.24311393211752));
#158624=CARTESIAN_POINT('Ctrl Pts',(-21.9509701153768,11.6537930500623,
3.0090335913358));
#158625=CARTESIAN_POINT('Ctrl Pts',(-21.9351613841381,11.3889377721737,
2.91771004900118));
#158626=CARTESIAN_POINT('Ctrl Pts',(-21.8880369349077,10.5774214126253,
2.72445713079606));
#158627=CARTESIAN_POINT('Ctrl Pts',(-21.8580091533467,10.0178534544547,
2.702508135162));
#158628=CARTESIAN_POINT('Ctrl Pts',(-21.8117350925593,9.20799888551045,
2.82936143448262));
#158629=CARTESIAN_POINT('Ctrl Pts',(-21.7966922808976,8.9505832899176,2.89469190842999));
#158630=CARTESIAN_POINT('Ctrl Pts',(-21.7658144070032,8.42862069443619,
3.08034542418168));
#158631=CARTESIAN_POINT('Ctrl Pts',(-21.7499354473133,8.16689659842979,
3.20462489799745));
#158632=CARTESIAN_POINT('Ctrl Pts',(-21.7181513147124,7.68071999843214,
3.49931712327065));
#158633=CARTESIAN_POINT('Ctrl Pts',(-21.7023403176168,7.456512124172,3.66736853387015));
#158634=CARTESIAN_POINT('Ctrl Pts',(-21.6552296339294,6.84146664781248,
4.23062311346996));
#158635=CARTESIAN_POINT('Ctrl Pts',(-21.6252062531605,6.50952114646976,
4.68130093424691));
#158636=CARTESIAN_POINT('Ctrl Pts',(-21.5789403259214,6.16021652511212,
5.42260242657841));
#158637=CARTESIAN_POINT('Ctrl Pts',(-21.5638981717868,6.06985381932021,
5.67234174953908));
#158638=CARTESIAN_POINT('Ctrl Pts',(-21.5345482489233,5.93749382557748,
6.18221655998195));
#158639=CARTESIAN_POINT('Ctrl Pts',(-21.5201589270318,5.89519802892576,
6.44109555311767));
#158640=CARTESIAN_POINT('Ctrl Pts',(-21.4828396833504,5.84845620697068,
7.10860567556486));
#158641=CARTESIAN_POINT('Ctrl Pts',(-21.4596577911668,5.87839873192986,
7.51696953547816));
#158642=CARTESIAN_POINT('Ctrl Pts',(-21.423550649416,6.01694477422831,8.14752324270353));
#158643=CARTESIAN_POINT('Ctrl Pts',(-21.4104259251066,6.08748232390585,
8.37550581925328));
#158644=CARTESIAN_POINT('Ctrl Pts',(-21.3655742102444,6.38912305546613,
9.12238960843889));
#158645=CARTESIAN_POINT('Ctrl Pts',(-21.3333897070469,6.70441487023999,
9.60072283825932));
#158646=CARTESIAN_POINT('Ctrl Pts',(-21.2868929381845,7.29624627282401,
10.1969137484751));
#158647=CARTESIAN_POINT('Ctrl Pts',(-21.2718238897837,7.50656447427855,
10.3716151107222));
#158648=CARTESIAN_POINT('Ctrl Pts',(-21.2355726264431,8.04030007418018,
10.7346101683361));
#158649=CARTESIAN_POINT('Ctrl Pts',(-21.2143744670667,8.3746396975226,10.9028895836668));
#158650=CARTESIAN_POINT('Ctrl Pts',(-21.1804533596015,8.9500000326423,11.10340386045));
#158651=CARTESIAN_POINT('Ctrl Pts',(-21.1673753465103,9.17950354419723,
11.1625292427343));
#158652=CARTESIAN_POINT('Ctrl Pts',(-21.1407215400377,9.6494148452743,11.2426807480191));
#158653=CARTESIAN_POINT('Ctrl Pts',(-21.1271864912783,9.88908519110593,
11.2629817136974));
#158654=CARTESIAN_POINT('Ctrl Pts',(-21.1136182899058,10.1291755310197,
11.2629999876519));
#158655=CARTESIAN_POINT('Origin',(-23.734,10.1295,7.));
#158656=CARTESIAN_POINT('',(-19.2041804192452,10.1294996037974,11.263));
#158657=CARTESIAN_POINT('',(-19.613681670589,10.1296816520865,11.2629999961298));
#158658=CARTESIAN_POINT('',(-23.734,10.1295,11.263));
#158659=CARTESIAN_POINT('Ctrl Pts',(-19.2041804192453,10.1294996037957,
11.263));
#158660=CARTESIAN_POINT('Ctrl Pts',(-19.2091555077248,10.0412386223353,
11.262999991797));
#158661=CARTESIAN_POINT('Ctrl Pts',(-19.2141495951209,9.95288587610765,
11.2602590200357));
#158662=CARTESIAN_POINT('Ctrl Pts',(-19.2344704309081,9.594334766552,11.2379329597718));
#158663=CARTESIAN_POINT('Ctrl Pts',(-19.2496908269967,9.32630807408874,
11.195398846032));
#158664=CARTESIAN_POINT('Ctrl Pts',(-19.2797045996433,8.80247160325071,
11.0601954801443));
#158665=CARTESIAN_POINT('Ctrl Pts',(-19.2946346564539,8.54783738766795,
10.9679379581973));
#158666=CARTESIAN_POINT('Ctrl Pts',(-19.3315996706072,7.95264534116758,
10.6858323724252));
#158667=CARTESIAN_POINT('Ctrl Pts',(-19.3536979505227,7.62600903500464,
10.4722620550939));
#158668=CARTESIAN_POINT('Ctrl Pts',(-19.3877232763041,7.16394309676322,
10.0706208008373));
#158669=CARTESIAN_POINT('Ctrl Pts',(-19.4000643592666,7.00688143635039,
9.91075471545546));
#158670=CARTESIAN_POINT('Ctrl Pts',(-19.4357313461682,6.59599208944473,
9.4208009938086));
#158671=CARTESIAN_POINT('Ctrl Pts',(-19.4593951127358,6.37691098361786,
9.06495067689065));
#158672=CARTESIAN_POINT('Ctrl Pts',(-19.4958348981863,6.11940880274535,
8.46570780361107));
#158673=CARTESIAN_POINT('Ctrl Pts',(-19.5088537924435,6.04426507456067,
8.24096309539799));
#158674=CARTESIAN_POINT('Ctrl Pts',(-19.5535524077618,5.85366486086651,
7.46032192478212));
#158675=CARTESIAN_POINT('Ctrl Pts',(-19.5857113991186,5.83041185246494,
6.88816788272283));
#158676=CARTESIAN_POINT('Ctrl Pts',(-19.6323145553016,5.96283750508647,
6.05828516392695));
#158677=CARTESIAN_POINT('Ctrl Pts',(-19.6474509864785,6.03178219950232,
5.79310020348745));
#158678=CARTESIAN_POINT('Ctrl Pts',(-19.6857655215158,6.26573850417946,
5.15310490708459));
#158679=CARTESIAN_POINT('Ctrl Pts',(-19.7088843434601,6.46014558211258,
4.79193919500421));
#158680=CARTESIAN_POINT('Ctrl Pts',(-19.7465491137239,6.86432665940929,
4.24583352824216));
#158681=CARTESIAN_POINT('Ctrl Pts',(-19.7615422170789,7.04619287785323,
4.04365037828345));
#158682=CARTESIAN_POINT('Ctrl Pts',(-19.7984847782363,7.53088218012923,
3.59854141372588));
#158683=CARTESIAN_POINT('Ctrl Pts',(-19.8204696525764,7.85001162023237,
3.37692371205805));
#158684=CARTESIAN_POINT('Ctrl Pts',(-19.8566369314541,8.42965415314089,
3.08167682554085));
#158685=CARTESIAN_POINT('Ctrl Pts',(-19.8711968764263,8.67527171508076,
2.98403797096035));
#158686=CARTESIAN_POINT('Ctrl Pts',(-19.9081683831554,9.30841328477263,
2.7981068549328));
#158687=CARTESIAN_POINT('Ctrl Pts',(-19.9307401674725,9.70220546686087,
2.74000951869332));
#158688=CARTESIAN_POINT('Ctrl Pts',(-19.9694380892079,10.3980406039924,
2.73492315147449));
#158689=CARTESIAN_POINT('Ctrl Pts',(-19.9858727647485,10.6971367123354,
2.76434369637872));
#158690=CARTESIAN_POINT('Ctrl Pts',(-20.0227662733845,11.3432954392777,
2.89762198974648));
#158691=CARTESIAN_POINT('Ctrl Pts',(-20.0432699897383,11.6852809105655,
3.01473420416989));
#158692=CARTESIAN_POINT('Ctrl Pts',(-20.076651410723,12.2202683677404,3.27742892102962));
#158693=CARTESIAN_POINT('Ctrl Pts',(-20.0896708823895,12.4230772446439,
3.39883984538454));
#158694=CARTESIAN_POINT('Ctrl Pts',(-20.1334004236417,13.060990745914,3.85657432071279));
#158695=CARTESIAN_POINT('Ctrl Pts',(-20.1645279866838,13.441139920168,4.25996144938882));
#158696=CARTESIAN_POINT('Ctrl Pts',(-20.2100247655609,13.8790518431926,
4.95364727143574));
#158697=CARTESIAN_POINT('Ctrl Pts',(-20.2250273884282,14.0015916712933,
5.19622618956876));
#158698=CARTESIAN_POINT('Ctrl Pts',(-20.260882647435,14.2334407076506,5.789709985387));
#158699=CARTESIAN_POINT('Ctrl Pts',(-20.2818214487302,14.322168679465,6.14637236301619));
#158700=CARTESIAN_POINT('Ctrl Pts',(-20.3135537072225,14.3880112771085,
6.71538442436535));
#158701=CARTESIAN_POINT('Ctrl Pts',(-20.3248315747683,14.3968038232362,
6.9222480698235));
#158702=CARTESIAN_POINT('Ctrl Pts',(-20.3546688285941,14.380365048869,7.46552067577716));
#158703=CARTESIAN_POINT('Ctrl Pts',(-20.3733100925241,14.3303361250923,
7.79969984624028));
#158704=CARTESIAN_POINT('Ctrl Pts',(-20.417539114031,14.1239496172783,8.55441328809823));
#158705=CARTESIAN_POINT('Ctrl Pts',(-20.4428344074042,13.939685282225,8.96323388419608));
#158706=CARTESIAN_POINT('Ctrl Pts',(-20.4837268841908,13.5544044546243,
9.55136430710921));
#158707=CARTESIAN_POINT('Ctrl Pts',(-20.4987792036827,13.3941307270601,
9.75347485757442));
#158708=CARTESIAN_POINT('Ctrl Pts',(-20.5178127710289,13.161755636317,9.99748555588612));
#158709=CARTESIAN_POINT('Ctrl Pts',(-20.522248843943,13.1053061725239,10.0535344672164));
#158710=CARTESIAN_POINT('Ctrl Pts',(-20.5321349407436,12.9736042138546,
10.1771785327503));
#158711=CARTESIAN_POINT('Ctrl Pts',(-20.5375188011386,12.8974492660982,
10.2437401275997));
#158712=CARTESIAN_POINT('Ctrl Pts',(-20.558580141542,12.5853323786389,10.4975358412307));
#158713=CARTESIAN_POINT('Ctrl Pts',(-20.5735495753211,12.3321844091471,
10.6622488002918));
#158714=CARTESIAN_POINT('Ctrl Pts',(-20.5972520006835,11.923575169114,10.8702994496326));
#158715=CARTESIAN_POINT('Ctrl Pts',(-20.6055199827159,11.7795335659103,
10.9338666400614));
#158716=CARTESIAN_POINT('Ctrl Pts',(-20.618904508283,11.5481062279498,11.0210475063173));
#158717=CARTESIAN_POINT('Ctrl Pts',(-20.6238506098718,11.4629173548294,
11.0500942269107));
#158718=CARTESIAN_POINT('Ctrl Pts',(-20.6339717950465,11.2898491377814,
11.1030527573785));
#158719=CARTESIAN_POINT('Ctrl Pts',(-20.6391462195046,11.2019957859215,
11.1268878189299));
#158720=CARTESIAN_POINT('Ctrl Pts',(-20.6537883564757,10.9555454474256,
11.1853500835783));
#158721=CARTESIAN_POINT('Ctrl Pts',(-20.6634370025332,10.7956451865527,
11.2137569600568));
#158722=CARTESIAN_POINT('Ctrl Pts',(-20.6836076701493,10.4657507135338,
11.2531160154837));
#158723=CARTESIAN_POINT('Ctrl Pts',(-20.6941318382673,10.2959301957534,
11.2631390120574));
#158724=CARTESIAN_POINT('Ctrl Pts',(-20.7046820180537,10.1259765948704,
11.2629985439379));
#158725=CARTESIAN_POINT('Ctrl Pts',(-19.613681670589,10.1296816520865,11.2629999961298));
#158726=CARTESIAN_POINT('Ctrl Pts',(-19.6210625559268,9.99792696780947,
11.2630056103717));
#158727=CARTESIAN_POINT('Ctrl Pts',(-19.6284434412646,9.86616452721088,
11.2568987546168));
#158728=CARTESIAN_POINT('Ctrl Pts',(-19.6358243266025,9.73495915245449,
11.2447033488358));
#158729=CARTESIAN_POINT('Ctrl Pts',(-19.6432038414137,9.60377814069074,
11.2325102075702));
#158730=CARTESIAN_POINT('Ctrl Pts',(-19.6505833562249,9.47315430553389,
11.2142308037361));
#158731=CARTESIAN_POINT('Ctrl Pts',(-19.6579628710361,9.34364777489142,
11.1899409638194));
#158732=CARTESIAN_POINT('Ctrl Pts',(-19.665341452104,9.21415763094539,11.1656541973403));
#158733=CARTESIAN_POINT('Ctrl Pts',(-19.6727200331718,9.0857848227637,11.1353585705236));
#158734=CARTESIAN_POINT('Ctrl Pts',(-19.6800986142396,8.95908014795422,
11.0991811828629));
#158735=CARTESIAN_POINT('Ctrl Pts',(-19.6849303155029,8.87611038293851,
11.0754912175352));
#158736=CARTESIAN_POINT('Ctrl Pts',(-19.6897620167663,8.79385571635695,
11.049280203234));
#158737=CARTESIAN_POINT('Ctrl Pts',(-19.6945937180296,8.71246771439215,
11.0205955406563));
#158738=CARTESIAN_POINT('Ctrl Pts',(-19.7016228891401,8.59406424510147,
10.9788650216284));
#158739=CARTESIAN_POINT('Ctrl Pts',(-19.7086520602506,8.47745739883753,
10.9318830738138));
#158740=CARTESIAN_POINT('Ctrl Pts',(-19.7156812313611,8.36312882780601,
10.8798327131517));
#158741=CARTESIAN_POINT('Ctrl Pts',(-19.7227086284805,8.24882911051486,
10.82779548873));
#158742=CARTESIAN_POINT('Ctrl Pts',(-19.7297360255998,8.13680687283187,
10.7706925591275));
#158743=CARTESIAN_POINT('Ctrl Pts',(-19.7367634227191,8.02752294555477,
10.7087547050979));
#158744=CARTESIAN_POINT('Ctrl Pts',(-19.7437922455919,7.91821684620777,
10.6468042848066));
#158745=CARTESIAN_POINT('Ctrl Pts',(-19.7508210684647,7.8116505045704,10.5800171656424));
#158746=CARTESIAN_POINT('Ctrl Pts',(-19.7578498913375,7.70825937959702,
10.5086696707029));
#158747=CARTESIAN_POINT('Ctrl Pts',(-19.7648793838462,7.60485840455196,
10.4373153784882));
#158748=CARTESIAN_POINT('Ctrl Pts',(-19.7719088763549,7.50463356199163,
10.3614000686881));
#158749=CARTESIAN_POINT('Ctrl Pts',(-19.7789383688636,7.40798992434636,
10.2812424336089));
#158750=CARTESIAN_POINT('Ctrl Pts',(-19.7859724420486,7.31128331014651,
10.2010325648618));
#158751=CARTESIAN_POINT('Ctrl Pts',(-19.7930065152336,7.21816285464981,
10.1165750994141));
#158752=CARTESIAN_POINT('Ctrl Pts',(-19.8000405884186,7.12899939384763,
10.0282280482948));
#158753=CARTESIAN_POINT('Ctrl Pts',(-19.8036735132583,7.08294867145319,
9.98259898131086));
#158754=CARTESIAN_POINT('Ctrl Pts',(-19.807306438098,7.03795286658765,9.93593298706528));
#158755=CARTESIAN_POINT('Ctrl Pts',(-19.8109393629378,6.99405904894667,
9.88828306134593));
#158756=CARTESIAN_POINT('Ctrl Pts',(-19.8185514682813,6.90208787460305,
9.78844167453286));
#158757=CARTESIAN_POINT('Ctrl Pts',(-19.8261635736248,6.81489782850554,
9.68421427120516));
#158758=CARTESIAN_POINT('Ctrl Pts',(-19.8337756789683,6.73287352582023,
9.57606242061428));
#158759=CARTESIAN_POINT('Ctrl Pts',(-19.8415681230414,6.64890598169537,
9.46534833967273));
#158760=CARTESIAN_POINT('Ctrl Pts',(-19.8493605671145,6.5703521935622,9.35052175498863));
#158761=CARTESIAN_POINT('Ctrl Pts',(-19.8571530111877,6.49757984993105,
9.23211223363054));
#158762=CARTESIAN_POINT('Ctrl Pts',(-19.8647591278018,6.42654758755655,
9.11653403772446));
#158763=CARTESIAN_POINT('Ctrl Pts',(-19.872365244416,6.36102356679838,8.99754254531327));
#158764=CARTESIAN_POINT('Ctrl Pts',(-19.8799713610301,6.30130558280906,
8.8756589519921));
#158765=CARTESIAN_POINT('Ctrl Pts',(-19.8878569688327,6.23939322668899,
8.74929667498954));
#158766=CARTESIAN_POINT('Ctrl Pts',(-19.8957425766354,6.18372190273754,
8.61982593912762));
#158767=CARTESIAN_POINT('Ctrl Pts',(-19.903628184438,6.13457147332775,8.48785586223272));
#158768=CARTESIAN_POINT('Ctrl Pts',(-19.9115137922407,6.08542104391795,
8.35588578533781));
#158769=CARTESIAN_POINT('Ctrl Pts',(-19.9193994000433,6.04279165902778,
8.22141665147341));
#158770=CARTESIAN_POINT('Ctrl Pts',(-19.927285007846,6.00690792403289,8.085082289586));
#158771=CARTESIAN_POINT('Ctrl Pts',(-19.9343237861388,5.97487771643589,
7.96338877260736));
#158772=CARTESIAN_POINT('Ctrl Pts',(-19.9413625644316,5.94823387545845,
7.8402524200153));
#158773=CARTESIAN_POINT('Ctrl Pts',(-19.9484013427244,5.92708903886797,
7.71617812990721));
#158774=CARTESIAN_POINT('Ctrl Pts',(-19.9554399109056,5.90594483346336,
7.59210754349001));
#158775=CARTESIAN_POINT('Ctrl Pts',(-19.9624784790867,5.89029936842274,
7.46709945251523));
#158776=CARTESIAN_POINT('Ctrl Pts',(-19.9695170472678,5.8802139040895,7.3416674920177));
#158777=CARTESIAN_POINT('Ctrl Pts',(-19.9765593081639,5.87012314851751,
7.21616972488726));
#158778=CARTESIAN_POINT('Ctrl Pts',(-19.9836015690599,5.86559825316507,
7.0902480255059));
#158779=CARTESIAN_POINT('Ctrl Pts',(-19.990643829956,5.86664848269717,6.96441992932841));
#158780=CARTESIAN_POINT('Ctrl Pts',(-19.9976880482936,5.86769900414732,
6.83855685842447));
#158781=CARTESIAN_POINT('Ctrl Pts',(-20.0047322666312,5.87432772657293,
6.71278782503369));
#158782=CARTESIAN_POINT('Ctrl Pts',(-20.0117764849689,5.88649181534104,
6.58762814727832));
#158783=CARTESIAN_POINT('Ctrl Pts',(-20.0188271374083,5.89866701463715,
6.46235415022382));
#158784=CARTESIAN_POINT('Ctrl Pts',(-20.0258777898477,5.91638763336263,
6.33769100055036));
#158785=CARTESIAN_POINT('Ctrl Pts',(-20.0329284422871,5.93955916974701,
6.21414706275352));
#158786=CARTESIAN_POINT('Ctrl Pts',(-20.0364958457761,5.95128322230163,
6.15163780158474));
#158787=CARTESIAN_POINT('Ctrl Pts',(-20.0400632492651,5.96440191628728,
6.08941489423676));
#158788=CARTESIAN_POINT('Ctrl Pts',(-20.0436306527542,5.97889809135828,
6.02754290789789));
#158789=CARTESIAN_POINT('Ctrl Pts',(-20.0506540818166,6.00743785637264,
5.90573064070087));
#158790=CARTESIAN_POINT('Ctrl Pts',(-20.0576775108791,6.04137122992328,
5.78506070393765));
#158791=CARTESIAN_POINT('Ctrl Pts',(-20.0647009399416,6.08058632073389,
5.6660333520467));
#158792=CARTESIAN_POINT('Ctrl Pts',(-20.0717185423857,6.11976887880798,
5.54710474493479));
#158793=CARTESIAN_POINT('Ctrl Pts',(-20.0787361448298,6.16422430917893,
5.42981637531585));
#158794=CARTESIAN_POINT('Ctrl Pts',(-20.085753747274,6.21379041548669,5.3146550947208));
#158795=CARTESIAN_POINT('Ctrl Pts',(-20.0927670920274,6.2633264492517,5.19956368430097));
#158796=CARTESIAN_POINT('Ctrl Pts',(-20.0997804367809,6.31796683139565,
5.08659714716067));
#158797=CARTESIAN_POINT('Ctrl Pts',(-20.1067937815343,6.37750071407498,
4.97622373805349));
#158798=CARTESIAN_POINT('Ctrl Pts',(-20.1138574549108,6.43746181920613,
4.86505827581068));
#158799=CARTESIAN_POINT('Ctrl Pts',(-20.1209211282873,6.5023867959048,4.75652367863071));
#158800=CARTESIAN_POINT('Ctrl Pts',(-20.1279848016638,6.57201228474143,
4.65107468067111));
#158801=CARTESIAN_POINT('Ctrl Pts',(-20.1349957589147,6.64111815923273,
4.54641264755664));
#158802=CARTESIAN_POINT('Ctrl Pts',(-20.1420067161656,6.71485438329882,
4.44479062478944));
#158803=CARTESIAN_POINT('Ctrl Pts',(-20.1490176734164,6.79291940437145,
4.34662499279219));
#158804=CARTESIAN_POINT('Ctrl Pts',(-20.1560293038896,6.87099192158304,
4.2484499345089));
#158805=CARTESIAN_POINT('Ctrl Pts',(-20.1630409343627,6.95339382288946,
4.15373223076921));
#158806=CARTESIAN_POINT('Ctrl Pts',(-20.1700525648358,7.03978297499938,
4.06285551846333));
#158807=CARTESIAN_POINT('Ctrl Pts',(-20.1770662859279,7.12619788528295,
3.97195170995291));
#158808=CARTESIAN_POINT('Ctrl Pts',(-20.1840800070199,7.21660214710082,
3.88489145349599));
#158809=CARTESIAN_POINT('Ctrl Pts',(-20.191093728112,7.3106167200912,3.80202156757576));
#158810=CARTESIAN_POINT('Ctrl Pts',(-20.1981960793168,7.4058193246704,3.71810448185337));
#158811=CARTESIAN_POINT('Ctrl Pts',(-20.2052984305217,7.50472380869981,
3.63848467191371));
#158812=CARTESIAN_POINT('Ctrl Pts',(-20.2124007817266,7.6069029600472,3.5634794960569));
#158813=CARTESIAN_POINT('Ctrl Pts',(-20.2194267016631,7.70798252029948,
3.4892814811754));
#158814=CARTESIAN_POINT('Ctrl Pts',(-20.2264526215996,7.81226625486711,
3.41959943125368));
#158815=CARTESIAN_POINT('Ctrl Pts',(-20.2334785415361,7.91931293289363,
3.3546958798482));
#158816=CARTESIAN_POINT('Ctrl Pts',(-20.2406191083752,8.02810636724196,
3.28873325131098));
#158817=CARTESIAN_POINT('Ctrl Pts',(-20.2477596752143,8.13975333669771,
3.22770663540868));
#158818=CARTESIAN_POINT('Ctrl Pts',(-20.2549002420533,8.25376708692567,
3.17184182160537));
#158819=CARTESIAN_POINT('Ctrl Pts',(-20.2620408088924,8.36778083715362,
3.11597700780207));
#158820=CARTESIAN_POINT('Ctrl Pts',(-20.2691813757315,8.48416096703565,
3.06527411157802));
#158821=CARTESIAN_POINT('Ctrl Pts',(-20.2763219425705,8.60240284429547,
3.0199066245829));
#158822=CARTESIAN_POINT('Ctrl Pts',(-20.2831124685135,8.71484833401245,
2.97676311730259));
#158823=CARTESIAN_POINT('Ctrl Pts',(-20.2899029944564,8.82935140599041,
2.93830145149597));
#158824=CARTESIAN_POINT('Ctrl Pts',(-20.2966935203994,8.94547734886698,
2.90472719326246));
#158825=CARTESIAN_POINT('Ctrl Pts',(-20.3034748353439,9.06144577288687,
2.87119847677993));
#158826=CARTESIAN_POINT('Ctrl Pts',(-20.3102561502883,9.17903229471747,
2.842544107233));
#158827=CARTESIAN_POINT('Ctrl Pts',(-20.3170374652328,9.29778142242843,
2.81892200410919));
#158828=CARTESIAN_POINT('Ctrl Pts',(-20.3238114588109,9.41640234404969,
2.79532540430932));
#158829=CARTESIAN_POINT('Ctrl Pts',(-20.330585452389,9.53618296819803,2.77675035206636));
#158830=CARTESIAN_POINT('Ctrl Pts',(-20.3373594459671,9.65665251765119,
2.76330503122583));
#158831=CARTESIAN_POINT('Ctrl Pts',(-20.3441279982186,9.77702529787156,
2.74987051056998));
#158832=CARTESIAN_POINT('Ctrl Pts',(-20.3508965504701,9.89808548802565,
2.74155757451038));
#158833=CARTESIAN_POINT('Ctrl Pts',(-20.3576651027216,10.0193527277818,
2.73842322861328));
#158834=CARTESIAN_POINT('Ctrl Pts',(-20.3644308259848,10.1405692826068,
2.73529019274934));
#158835=CARTESIAN_POINT('Ctrl Pts',(-20.371196549248,10.2619922966189,2.73733145918129));
#158836=CARTESIAN_POINT('Ctrl Pts',(-20.3779622725112,10.383137499644,2.74455207777438));
#158837=CARTESIAN_POINT('Ctrl Pts',(-20.384726762254,10.5042606155877,2.75177137991097));
#158838=CARTESIAN_POINT('Ctrl Pts',(-20.3914912519967,10.6251056025061,
2.7641681330934));
#158839=CARTESIAN_POINT('Ctrl Pts',(-20.3982557417395,10.7451902242561,
2.78169529932278));
#158840=CARTESIAN_POINT('Ctrl Pts',(-20.405020688733,10.8652829632157,2.79922365031404));
#158841=CARTESIAN_POINT('Ctrl Pts',(-20.4117856357265,10.9846148196652,
2.82188304272845));
#158842=CARTESIAN_POINT('Ctrl Pts',(-20.41855058272,11.1027114907248,2.84957491402132));
#158843=CARTESIAN_POINT('Ctrl Pts',(-20.4253176780028,11.2208456647849,
2.87727557919678));
#158844=CARTESIAN_POINT('Ctrl Pts',(-20.4320847732856,11.3377434657248,
2.91001180325871));
#158845=CARTESIAN_POINT('Ctrl Pts',(-20.4388518685683,11.4529443165418,
2.9476347473342));
#158846=CARTESIAN_POINT('Ctrl Pts',(-20.4456269530807,11.5682811734314,
2.98530210904052));
#158847=CARTESIAN_POINT('Ctrl Pts',(-20.4524020375931,11.6819166829018,
3.0278675742583));
#158848=CARTESIAN_POINT('Ctrl Pts',(-20.4591771221056,11.7934087946616,
3.07513356621555));
#158849=CARTESIAN_POINT('Ctrl Pts',(-20.4659567627322,11.9049758827261,
3.12243134364499));
#158850=CARTESIAN_POINT('Ctrl Pts',(-20.4727364033589,12.0143963278875,
3.1744357569713));
#158851=CARTESIAN_POINT('Ctrl Pts',(-20.4795160439856,12.1212529943158,
3.23090342261781));
#158852=CARTESIAN_POINT('Ctrl Pts',(-20.4863065022887,12.2282801625317,
3.28746118875372));
#158853=CARTESIAN_POINT('Ctrl Pts',(-20.4930969605919,12.3327350284989,
3.34849620756881));
#158854=CARTESIAN_POINT('Ctrl Pts',(-20.499887418895,12.434229583985,3.41372190917881));
#158855=CARTESIAN_POINT('Ctrl Pts',(-20.5029293567257,12.479696342509,3.44294122257403));
#158856=CARTESIAN_POINT('Ctrl Pts',(-20.5059712945563,12.5245694743666,
3.47300098129164));
#158857=CARTESIAN_POINT('Ctrl Pts',(-20.5090132323869,12.5688163807365,
3.50387291497142));
#158858=CARTESIAN_POINT('Ctrl Pts',(-20.5160528500654,12.6712120645548,
3.57531639021697));
#158859=CARTESIAN_POINT('Ctrl Pts',(-20.5230924677439,12.7706045269319,
3.65135814019731));
#158860=CARTESIAN_POINT('Ctrl Pts',(-20.5301320854224,12.8665642076717,
3.73172086212295));
#158861=CARTESIAN_POINT('Ctrl Pts',(-20.5371627173815,12.9624014006857,
3.81198100505939));
#158862=CARTESIAN_POINT('Ctrl Pts',(-20.5441933493406,13.0548142404394,
3.89655089391907));
#158863=CARTESIAN_POINT('Ctrl Pts',(-20.5512239812998,13.1434028817285,
3.98511054605499));
#158864=CARTESIAN_POINT('Ctrl Pts',(-20.5582472086855,13.2318982225716,
4.07357692827592));
#158865=CARTESIAN_POINT('Ctrl Pts',(-20.5652704360712,13.3165771118334,
4.16602443564554));
#158866=CARTESIAN_POINT('Ctrl Pts',(-20.5722936634569,13.3970737490667,
4.26209372066711));
#158867=CARTESIAN_POINT('Ctrl Pts',(-20.579352449238,13.477977938426,4.35864940167621));
#158868=CARTESIAN_POINT('Ctrl Pts',(-20.5864112350191,13.5546571020791,
4.45886338581479));
#158869=CARTESIAN_POINT('Ctrl Pts',(-20.5934700208002,13.6267777203579,
4.56233358584726));
#158870=CARTESIAN_POINT('Ctrl Pts',(-20.6004831025417,13.6984313739637,
4.6651338397634));
#158871=CARTESIAN_POINT('Ctrl Pts',(-20.6074961842832,13.7655851192017,
4.77114794331499));
#158872=CARTESIAN_POINT('Ctrl Pts',(-20.6145092660247,13.8279529364795,
4.87994932215142));
#158873=CARTESIAN_POINT('Ctrl Pts',(-20.6215201005457,13.8903007690717,
4.98871583747262));
#158874=CARTESIAN_POINT('Ctrl Pts',(-20.6285309350668,13.947865534977,5.10026751473464));
#158875=CARTESIAN_POINT('Ctrl Pts',(-20.6355417695879,14.000405778642,5.214150775436));
#158876=CARTESIAN_POINT('Ctrl Pts',(-20.6425517747268,14.0529398067936,
5.32802056374194));
#158877=CARTESIAN_POINT('Ctrl Pts',(-20.6495617798658,14.1004503352034,
5.44422103493076));
#158878=CARTESIAN_POINT('Ctrl Pts',(-20.6565717850048,14.1427430711648,
5.56227643416836));
#158879=CARTESIAN_POINT('Ctrl Pts',(-20.6636661797713,14.1855449463016,
5.68175303795214));
#158880=CARTESIAN_POINT('Ctrl Pts',(-20.6707605745379,14.2230024133749,
5.80312915290586));
#158881=CARTESIAN_POINT('Ctrl Pts',(-20.6778549693044,14.2549654534142,
5.92589395649855));
#158882=CARTESIAN_POINT('Ctrl Pts',(-20.6848700180614,14.2865710084581,
6.04728571875378));
#158883=CARTESIAN_POINT('Ctrl Pts',(-20.6918850668184,14.3128043681359,
6.17003487300886));
#158884=CARTESIAN_POINT('Ctrl Pts',(-20.6989001155754,14.3335717231044,
6.29363610865666));
#158885=CARTESIAN_POINT('Ctrl Pts',(-20.7060341833467,14.3546914220416,
6.41933439277077));
#158886=CARTESIAN_POINT('Ctrl Pts',(-20.713168251118,14.37015788043,6.5459135246403));
#158887=CARTESIAN_POINT('Ctrl Pts',(-20.7203023188893,14.3799273655978,
6.6728361117461));
#158888=CARTESIAN_POINT('Ctrl Pts',(-20.7274363866606,14.3896968507655,
6.79975869885191));
#158889=CARTESIAN_POINT('Ctrl Pts',(-20.7345704544319,14.3937693782952,
6.92702432229997));
#158890=CARTESIAN_POINT('Ctrl Pts',(-20.7417045222032,14.3921567579672,
7.05409587559758));
#158891=CARTESIAN_POINT('Ctrl Pts',(-20.7487553738306,14.3905629482322,
7.17968518832687));
#158892=CARTESIAN_POINT('Ctrl Pts',(-20.755806225458,14.3834131442202,7.30531135250305));
#158893=CARTESIAN_POINT('Ctrl Pts',(-20.7628570770854,14.3707114727388,
7.43045817858265));
#158894=CARTESIAN_POINT('Ctrl Pts',(-20.7699025977755,14.35801940461,7.55551038490363));
#158895=CARTESIAN_POINT('Ctrl Pts',(-20.7769481184657,14.339783866004,7.68008359541989));
#158896=CARTESIAN_POINT('Ctrl Pts',(-20.7839936391558,14.316060990687,7.80366415327441));
#158897=CARTESIAN_POINT('Ctrl Pts',(-20.7910351758234,14.2923515299169,
7.92717483017315));
#158898=CARTESIAN_POINT('Ctrl Pts',(-20.7980767124911,14.2631609851212,
8.0496935975355));
#158899=CARTESIAN_POINT('Ctrl Pts',(-20.8051182491587,14.2285969725616,
8.17071474302503));
#158900=CARTESIAN_POINT('Ctrl Pts',(-20.8121573620581,14.1940448572855,
8.29169423180984));
#158901=CARTESIAN_POINT('Ctrl Pts',(-20.8191964749575,14.1541230641496,
8.41117675831594));
#158902=CARTESIAN_POINT('Ctrl Pts',(-20.8262355878569,14.108989607831,8.52866983392907));
#158903=CARTESIAN_POINT('Ctrl Pts',(-20.8332745473014,14.0638571354359,
8.64616034815655));
#158904=CARTESIAN_POINT('Ctrl Pts',(-20.8403135067459,14.0135133592023,
8.76166113931436));
#158905=CARTESIAN_POINT('Ctrl Pts',(-20.8473524661904,13.9581651263394,
8.87469793576249));
#158906=CARTESIAN_POINT('Ctrl Pts',(-20.8509183664974,13.9301259989493,
8.93196178993535));
#158907=CARTESIAN_POINT('Ctrl Pts',(-20.8544842668044,13.9008033009508,
8.98859361159937));
#158908=CARTESIAN_POINT('Ctrl Pts',(-20.8580501671115,13.8702285225073,
9.04453396178702));
#158909=CARTESIAN_POINT('Ctrl Pts',(-20.8656423239006,13.8051317750523,
9.16363653698444));
#158910=CARTESIAN_POINT('Ctrl Pts',(-20.8732344806897,13.7343815652685,
9.27955752070515));
#158911=CARTESIAN_POINT('Ctrl Pts',(-20.8808266374789,13.6583076665164,
9.39179544542065));
#158912=CARTESIAN_POINT('Ctrl Pts',(-20.8886240686906,13.580176904863,9.50706802495553));
#158913=CARTESIAN_POINT('Ctrl Pts',(-20.8964214999023,13.4964306780399,
9.61845531819866));
#158914=CARTESIAN_POINT('Ctrl Pts',(-20.9042189311141,13.4074713236086,
9.72544913759181));
#158915=CARTESIAN_POINT('Ctrl Pts',(-20.9118275959575,13.3206655674334,
9.8298527661687));
#158916=CARTESIAN_POINT('Ctrl Pts',(-20.919436260801,13.2288963926095,9.93007301888403));
#158917=CARTESIAN_POINT('Ctrl Pts',(-20.9270449256444,13.1325767406681,
10.0256733283119));
#158918=CARTESIAN_POINT('Ctrl Pts',(-20.9349367400403,13.0326726403515,
10.1248313164367));
#158919=CARTESIAN_POINT('Ctrl Pts',(-20.9428285544362,12.9278730596348,
10.2190186506561));
#158920=CARTESIAN_POINT('Ctrl Pts',(-20.950720368832,12.8186793474327,10.3077913231251));
#158921=CARTESIAN_POINT('Ctrl Pts',(-20.9586121832279,12.7094856352306,
10.396563995594));
#158922=CARTESIAN_POINT('Ctrl Pts',(-20.9665039976238,12.5958980403162,
10.4799218091269));
#158923=CARTESIAN_POINT('Ctrl Pts',(-20.9743958120197,12.4784556130269,
10.5574677128583));
#158924=CARTESIAN_POINT('Ctrl Pts',(-20.9814299786755,12.3737763131122,
10.6265862682323));
#158925=CARTESIAN_POINT('Ctrl Pts',(-20.9884641453313,12.2659720439805,
10.6911283149499));
#158926=CARTESIAN_POINT('Ctrl Pts',(-20.9954983119871,12.1554741760127,
10.7508129303032));
#158927=CARTESIAN_POINT('Ctrl Pts',(-21.0025285897974,12.0450373968928,
10.810464548962));
#158928=CARTESIAN_POINT('Ctrl Pts',(-21.0095588676077,11.9319103223061,
10.8652639016021));
#158929=CARTESIAN_POINT('Ctrl Pts',(-21.016589145418,11.8165508198208,10.9149749081369));
#158930=CARTESIAN_POINT('Ctrl Pts',(-21.0236176753931,11.7012199974825,
10.9646735557508));
#158931=CARTESIAN_POINT('Ctrl Pts',(-21.0306462053682,11.5836582040373,
11.0092862208708));
#158932=CARTESIAN_POINT('Ctrl Pts',(-21.0376747353433,11.4643451254216,
11.0486241479221));
#158933=CARTESIAN_POINT('Ctrl Pts',(-21.0447021255488,11.345051395008,11.0879556958055));
#158934=CARTESIAN_POINT('Ctrl Pts',(-21.0517295157543,11.2240073113907,
11.1220140919123));
#158935=CARTESIAN_POINT('Ctrl Pts',(-21.0587569059598,11.1017091471191,
11.1506599926106));
#158936=CARTESIAN_POINT('Ctrl Pts',(-21.0657861500461,10.9793787196288,
11.179313450323));
#158937=CARTESIAN_POINT('Ctrl Pts',(-21.0728153941325,10.8557939254294,
11.2025514728704));
#158938=CARTESIAN_POINT('Ctrl Pts',(-21.0798446382189,10.7314627077289,
11.2202855233389));
#158939=CARTESIAN_POINT('Ctrl Pts',(-21.0834769111219,10.6672161248101,
11.2294493694347));
#158940=CARTESIAN_POINT('Ctrl Pts',(-21.0871091840249,10.6027703828996,
11.2371443975746));
#158941=CARTESIAN_POINT('Ctrl Pts',(-21.0907414569279,10.5381962379688,
11.2433638054108));
#158942=CARTESIAN_POINT('Ctrl Pts',(-21.0983881948149,10.4022533796668,
11.2564570345833));
#158943=CARTESIAN_POINT('Ctrl Pts',(-21.106034932702,10.2657163342166,11.2630102654163));
#158944=CARTESIAN_POINT('Ctrl Pts',(-21.113681670589,10.1291791134783,11.262999987923));
#158945=CARTESIAN_POINT('Origin',(-23.734,10.1295,7.));
#158946=CARTESIAN_POINT('',(-17.7339525171114,10.1295,11.263));
#158947=CARTESIAN_POINT('',(-18.1138504934428,10.1295003780334,11.263));
#158948=CARTESIAN_POINT('',(-23.734,10.1295,11.263));
#158949=CARTESIAN_POINT('',(-17.734,9.60084442449481,11.2300936493755));
#158950=CARTESIAN_POINT('Origin',(-17.734,10.1295,7.));
#158951=CARTESIAN_POINT('Ctrl Pts',(-17.734,9.60084442449481,11.2300936493755));
#158952=CARTESIAN_POINT('Ctrl Pts',(-17.7617000790389,9.11002742083171,
11.1687538382398));
#158953=CARTESIAN_POINT('Ctrl Pts',(-17.7887513666815,8.6336091385854,11.0224564453886));
#158954=CARTESIAN_POINT('Ctrl Pts',(-17.8283758438164,8.010079686466,10.7045055574008));
#158955=CARTESIAN_POINT('Ctrl Pts',(-17.8400356673621,7.83418479791178,
10.5981710316897));
#158956=CARTESIAN_POINT('Ctrl Pts',(-17.8640864842584,7.48374154752343,
10.3501251931301));
#158957=CARTESIAN_POINT('Ctrl Pts',(-17.8764309707687,7.31133675452661,
10.2064522936414));
#158958=CARTESIAN_POINT('Ctrl Pts',(-17.9198792988024,6.75185233693977,
9.6600686649743));
#158959=CARTESIAN_POINT('Ctrl Pts',(-17.9515705295498,6.43307107325946,
9.19565118676176));
#158960=CARTESIAN_POINT('Ctrl Pts',(-17.9980608413685,6.10246074027769,
8.42626318993039));
#158961=CARTESIAN_POINT('Ctrl Pts',(-18.0134821699885,6.01764435575489,
8.15927229438703));
#158962=CARTESIAN_POINT('Ctrl Pts',(-18.0446219329139,5.90228404118004,
7.61627701282578));
#158963=CARTESIAN_POINT('Ctrl Pts',(-18.0602607748556,5.87128772424761,
7.34172435081686));
#158964=CARTESIAN_POINT('Ctrl Pts',(-18.0972591962321,5.86109815311643,
6.68480301531689));
#158965=CARTESIAN_POINT('Ctrl Pts',(-18.1180605746812,5.90637601846631,
6.3044208662641));
#158966=CARTESIAN_POINT('Ctrl Pts',(-18.1543359347367,6.0683334091008,5.67659879469026));
#158967=CARTESIAN_POINT('Ctrl Pts',(-18.1694414484725,6.15917338165903,
5.42489206896729));
#158968=CARTESIAN_POINT('Ctrl Pts',(-18.2068265544821,6.44111102179745,
4.82637038093062));
#158969=CARTESIAN_POINT('Ctrl Pts',(-18.2284065883895,6.65801820869123,
4.49446631522699));
#158970=CARTESIAN_POINT('Ctrl Pts',(-18.2655853293336,7.09602773048975,
3.99251414384753));
#158971=CARTESIAN_POINT('Ctrl Pts',(-18.2809060786613,7.29373013801882,
3.80542228181663));
#158972=CARTESIAN_POINT('Ctrl Pts',(-18.3192560865802,7.82847773736109,
3.38838423076535));
#158973=CARTESIAN_POINT('Ctrl Pts',(-18.341548988857,8.18320909687546,3.18549702299022));
#158974=CARTESIAN_POINT('Ctrl Pts',(-18.3794638857893,8.81559460658373,
2.93532082146657));
#158975=CARTESIAN_POINT('Ctrl Pts',(-18.3948721589547,9.07899002309546,
2.85942216427453));
#158976=CARTESIAN_POINT('Ctrl Pts',(-18.4424258696319,9.90536277180713,
2.70528299904782));
#158977=CARTESIAN_POINT('Ctrl Pts',(-18.4731651406769,10.4780900647047,
2.71358801542172));
#158978=CARTESIAN_POINT('Ctrl Pts',(-18.5185046603243,11.2644782764602,
2.88400803732114));
#158979=CARTESIAN_POINT('Ctrl Pts',(-18.53198999126,11.4919602735929,2.95361063545592));
#158980=CARTESIAN_POINT('Ctrl Pts',(-18.5686148708944,12.0973915996452,
3.19573366261946));
#158981=CARTESIAN_POINT('Ctrl Pts',(-18.5911956664381,12.4578149803992,
3.40500412070652));
#158982=CARTESIAN_POINT('Ctrl Pts',(-18.6291092351267,12.9859944857833,
3.82489462925093));
#158983=CARTESIAN_POINT('Ctrl Pts',(-18.6438768977571,13.1743959422191,
4.00509425775862));
#158984=CARTESIAN_POINT('Ctrl Pts',(-18.6734351481004,13.5191402296173,
4.40120899021167));
#158985=CARTESIAN_POINT('Ctrl Pts',(-18.6880135235118,13.6740753746476,
4.61685847799688));
#158986=CARTESIAN_POINT('Ctrl Pts',(-18.7336176921056,14.0890532736973,
5.3253711472166));
#158987=CARTESIAN_POINT('Ctrl Pts',(-18.7652076931336,14.2735153696961,
5.85563052663519));
#158988=CARTESIAN_POINT('Ctrl Pts',(-18.8116050038436,14.3898807843215,
6.68309052149403));
#158989=CARTESIAN_POINT('Ctrl Pts',(-18.8270192336647,14.4014906778751,
6.96299679224388));
#158990=CARTESIAN_POINT('Ctrl Pts',(-18.8583536528325,14.3697681512779,
7.52086853484267));
#158991=CARTESIAN_POINT('Ctrl Pts',(-18.8742000416313,14.3265453993646,
7.79748518887851));
#158992=CARTESIAN_POINT('Ctrl Pts',(-18.9167049423928,14.1375265626357,
8.52800017652366));
#158993=CARTESIAN_POINT('Ctrl Pts',(-18.9425081846297,13.9423576196096,
8.96498868777149));
#158994=CARTESIAN_POINT('Ctrl Pts',(-18.9829336075695,13.5448823717088,
9.5626402559391));
#158995=CARTESIAN_POINT('Ctrl Pts',(-18.9967031462161,13.3936277925957,
9.75271330915583));
#158996=CARTESIAN_POINT('Ctrl Pts',(-19.034160076992,12.935590791635,10.2371238056325));
#158997=CARTESIAN_POINT('Ctrl Pts',(-19.0572543880736,12.5997652716431,
10.5001302140577));
#158998=CARTESIAN_POINT('Ctrl Pts',(-19.0957940148976,12.0032932316461,
10.8380143501432));
#158999=CARTESIAN_POINT('Ctrl Pts',(-19.1106329571733,11.7645652514517,
10.9456322875166));
#159000=CARTESIAN_POINT('Ctrl Pts',(-19.1519247247326,11.0703266384371,
11.184696243469));
#159001=CARTESIAN_POINT('Ctrl Pts',(-19.1775909176582,10.6012129243344,
11.2630000438411));
#159002=CARTESIAN_POINT('Ctrl Pts',(-19.2041804192453,10.1294996037957,
11.263));
#159003=CARTESIAN_POINT('Ctrl Pts',(-18.1138504934428,10.1295003780333,
11.263));
#159004=CARTESIAN_POINT('Ctrl Pts',(-18.1201664240278,10.0171997379224,
11.2630000099585));
#159005=CARTESIAN_POINT('Ctrl Pts',(-18.1264601646708,9.90482338535515,
11.2585625113639));
#159006=CARTESIAN_POINT('Ctrl Pts',(-18.1471939564367,9.5342147629796,11.2291849445822));
#159007=CARTESIAN_POINT('Ctrl Pts',(-18.1614510886987,9.27820419644792,
11.1851718184008));
#159008=CARTESIAN_POINT('Ctrl Pts',(-18.190679063517,8.77185199290599,11.04970983128));
#159009=CARTESIAN_POINT('Ctrl Pts',(-18.205722478305,8.52286768105405,10.9575348695707));
#159010=CARTESIAN_POINT('Ctrl Pts',(-18.2521528724009,7.78127034447633,
10.6014003031429));
#159011=CARTESIAN_POINT('Ctrl Pts',(-18.2823439987331,7.33072756467248,
10.2636080327611));
#159012=CARTESIAN_POINT('Ctrl Pts',(-18.3296550402369,6.77127318646973,
9.64075362893174));
#159013=CARTESIAN_POINT('Ctrl Pts',(-18.3454529965589,6.60541983307923,
9.41498111034329));
#159014=CARTESIAN_POINT('Ctrl Pts',(-18.3746159475739,6.33918555578304,
8.96607800534638));
#159015=CARTESIAN_POINT('Ctrl Pts',(-18.3879852293196,6.23352792098854,
8.74738335505999));
#159016=CARTESIAN_POINT('Ctrl Pts',(-18.4231228670393,6.00789011106766,
8.15655051036886));
#159017=CARTESIAN_POINT('Ctrl Pts',(-18.445300526248,5.91940671390389,7.77483965536696));
#159018=CARTESIAN_POINT('Ctrl Pts',(-18.482391861555,5.85950946605294,7.1168303996138));
#159019=CARTESIAN_POINT('Ctrl Pts',(-18.497354685792,5.86070678728025,6.84547915816173));
#159020=CARTESIAN_POINT('Ctrl Pts',(-18.5347943580174,5.92782518434814,
6.17387956069213));
#159021=CARTESIAN_POINT('Ctrl Pts',(-18.5577058978721,6.02501704398986,
5.77944802631504));
#159022=CARTESIAN_POINT('Ctrl Pts',(-18.6118397338822,6.38541040569196,
4.8864095166674));
#159023=CARTESIAN_POINT('Ctrl Pts',(-18.6422259979436,6.69442250090281,
4.4143285720778));
#159024=CARTESIAN_POINT('Ctrl Pts',(-18.7055321400725,7.47793199683672,
3.61529249690852));
#159025=CARTESIAN_POINT('Ctrl Pts',(-18.7359957244316,7.94522450923478,
3.2964889392701));
#159026=CARTESIAN_POINT('Ctrl Pts',(-18.7812347653197,8.68607200895231,
2.98133970829284));
#159027=CARTESIAN_POINT('Ctrl Pts',(-18.7951387550697,8.91921102446701,
2.90508648402335));
#159028=CARTESIAN_POINT('Ctrl Pts',(-18.8352464895255,9.61273249287762,
2.74269814882526));
#159029=CARTESIAN_POINT('Ctrl Pts',(-18.8606342384993,10.0822955872121,
2.71170935717385));
#159030=CARTESIAN_POINT('Ctrl Pts',(-18.9034985446018,10.8398949502786,
2.78635012991713));
#159031=CARTESIAN_POINT('Ctrl Pts',(-18.920172849714,11.1285598118538,2.84531682591275));
#159032=CARTESIAN_POINT('Ctrl Pts',(-18.9522999708127,11.6754893919508,
3.01738596676868));
#159033=CARTESIAN_POINT('Ctrl Pts',(-18.967703420322,11.9332242435038,3.12729058389462));
#159034=CARTESIAN_POINT('Ctrl Pts',(-19.0109361724726,12.6156088885913,
3.50127687237792));
#159035=CARTESIAN_POINT('Ctrl Pts',(-19.0393144976386,13.0074483977873,
3.81578754937372));
#159036=CARTESIAN_POINT('Ctrl Pts',(-19.0795464292398,13.4834803550414,
4.35915580258086));
#159037=CARTESIAN_POINT('Ctrl Pts',(-19.0918774504661,13.6174543555981,
4.53881822871678));
#159038=CARTESIAN_POINT('Ctrl Pts',(-19.1230581322882,13.9158838913541,
5.01266238566637));
#159039=CARTESIAN_POINT('Ctrl Pts',(-19.1421826533911,14.0607725750834,
5.31735360043846));
#159040=CARTESIAN_POINT('Ctrl Pts',(-19.1853242557598,14.3062974466496,
6.04429874103027));
#159041=CARTESIAN_POINT('Ctrl Pts',(-19.2087794214143,14.3814932447286,
6.47127597578725));
#159042=CARTESIAN_POINT('Ctrl Pts',(-19.2466684721848,14.3969497001182,
7.145096609166));
#159043=CARTESIAN_POINT('Ctrl Pts',(-19.2604707095446,14.381752049973,7.3879865648949));
#159044=CARTESIAN_POINT('Ctrl Pts',(-19.3005656529627,14.2768757074118,
8.09184703182885));
#159045=CARTESIAN_POINT('Ctrl Pts',(-19.3260305629335,14.1318180963956,
8.54087751131874));
#159046=CARTESIAN_POINT('Ctrl Pts',(-19.3679683490484,13.7896058996363,
9.20302695145331));
#159047=CARTESIAN_POINT('Ctrl Pts',(-19.3836501061341,13.6389632072953,
9.43585214398804));
#159048=CARTESIAN_POINT('Ctrl Pts',(-19.4148089165798,13.2931223158563,
9.87099362074104));
#159049=CARTESIAN_POINT('Ctrl Pts',(-19.430208841783,13.0983665680379,10.0719609623287));
#159050=CARTESIAN_POINT('Ctrl Pts',(-19.4735764674731,12.5025186741097,
10.576835535129));
#159051=CARTESIAN_POINT('Ctrl Pts',(-19.5021850689032,12.0653976838966,
10.8310913618801));
#159052=CARTESIAN_POINT('Ctrl Pts',(-19.5440264004416,11.3608570703204,
11.0888435365032));
#159053=CARTESIAN_POINT('Ctrl Pts',(-19.5576923663702,11.1205471605292,
11.1536376829205));
#159054=CARTESIAN_POINT('Ctrl Pts',(-19.5854566839399,10.6296085314679,
11.2409518821898));
#159055=CARTESIAN_POINT('Ctrl Pts',(-19.5996238369442,10.379883262343,11.262989129004));
#159056=CARTESIAN_POINT('Ctrl Pts',(-19.6137437660346,10.1296851569352,
11.262999995979));
#159057=CARTESIAN_POINT('Origin',(-18.734,-18.952,0.));
#159058=CARTESIAN_POINT('',(-20.7225805737622,-18.2258896078036,0.755484073133954));
#159059=CARTESIAN_POINT('',(-20.7225805737341,-18.2258896077265,0.534177427254549));
#159060=CARTESIAN_POINT('',(-20.7225805737622,-18.2258896078036,0.));
#159061=CARTESIAN_POINT('',(-20.8509997094771,-18.9508909130732,0.710943721022757));
#159062=CARTESIAN_POINT('Ctrl Pts',(-20.8509997094771,-18.9508909130732,
0.710943721022757));
#159063=CARTESIAN_POINT('Ctrl Pts',(-20.8509573783464,-18.8700902207682,
0.71578119702302));
#159064=CARTESIAN_POINT('Ctrl Pts',(-20.8462849658904,-18.7894513944425,
0.720618673023283));
#159065=CARTESIAN_POINT('Ctrl Pts',(-20.8370625267197,-18.7094778181125,
0.725456149023546));
#159066=CARTESIAN_POINT('Ctrl Pts',(-20.8275213698741,-18.6267404401649,
0.730460803041947));
#159067=CARTESIAN_POINT('Ctrl Pts',(-20.8131101401339,-18.5447154876357,
0.735465457060348));
#159068=CARTESIAN_POINT('Ctrl Pts',(-20.7939728278586,-18.463941654631,
0.74047011107875));
#159069=CARTESIAN_POINT('Ctrl Pts',(-20.7748355155832,-18.3831678216262,
0.745474765097151));
#159070=CARTESIAN_POINT('Ctrl Pts',(-20.7509723251239,-18.303645395105,
0.750479419115552));
#159071=CARTESIAN_POINT('Ctrl Pts',(-20.7225805737622,-18.2258896078036,
0.755484073133953));
#159072=CARTESIAN_POINT('',(-20.3539400851898,-17.5891048754966,2.1911925810487E-7));
#159073=CARTESIAN_POINT('Ctrl Pts',(-20.3539400851898,-17.5891048754966,
2.1911925810487E-7));
#159074=CARTESIAN_POINT('Ctrl Pts',(-20.3072931859159,-17.5336602703872,
0.00438523983104698));
#159075=CARTESIAN_POINT('Ctrl Pts',(-20.2577048501402,-17.4805043431566,
0.00877026054283585));
#159076=CARTESIAN_POINT('Ctrl Pts',(-20.2054284583706,-17.4299660674291,
0.0131552812546247));
#159077=CARTESIAN_POINT('Ctrl Pts',(-20.1532296863998,-17.3795028307521,
0.017533791103401));
#159078=CARTESIAN_POINT('Ctrl Pts',(-20.0983511257708,-17.3316498632894,
0.0219123009521774));
#159079=CARTESIAN_POINT('Ctrl Pts',(-20.0410859170619,-17.2867026075147,
0.0262908108009537));
#159080=CARTESIAN_POINT('Ctrl Pts',(-19.9838881021842,-17.241808248915,
0.030664167703297));
#159081=CARTESIAN_POINT('Ctrl Pts',(-19.9243095970083,-17.1998131057541,
0.0350375246056404));
#159082=CARTESIAN_POINT('Ctrl Pts',(-19.862678574843,-17.1609741278556,
0.0394108815079837));
#159083=CARTESIAN_POINT('Ctrl Pts',(-19.801086549423,-17.1221597251416,
0.0437814711888932));
#159084=CARTESIAN_POINT('Ctrl Pts',(-19.7374449915696,-17.0864977823031,
0.0481520608698027));
#159085=CARTESIAN_POINT('Ctrl Pts',(-19.6721120099387,-17.0542026302029,
0.0525226505507122));
#159086=CARTESIAN_POINT('Ctrl Pts',(-19.6067987309426,-17.0219172174345,
0.0568919221816862));
#159087=CARTESIAN_POINT('Ctrl Pts',(-19.5397954737533,-16.9929967935616,
0.0612611938126602));
#159088=CARTESIAN_POINT('Ctrl Pts',(-19.4714844671138,-16.9676094989227,
0.0656304654436342));
#159089=CARTESIAN_POINT('Ctrl Pts',(-19.4031714390129,-16.9422214530222,
0.0699998663702325));
#159090=CARTESIAN_POINT('Ctrl Pts',(-19.3335510382756,-16.9203669101752,
0.0743692672968309));
#159091=CARTESIAN_POINT('Ctrl Pts',(-19.2630233707279,-16.9021650619565,
0.0787386682234292));
#159092=CARTESIAN_POINT('Ctrl Pts',(-19.1924239083033,-16.883944684847,
0.0831125170583901));
#159093=CARTESIAN_POINT('Ctrl Pts',(-19.1209158041549,-16.8693845460032,
0.087486365893351));
#159094=CARTESIAN_POINT('Ctrl Pts',(-19.0489112989912,-16.8585531117872,
0.0918602147283118));
#159095=CARTESIAN_POINT('Ctrl Pts',(-18.9768669711113,-16.8477156871526,
0.0962364825583059));
#159096=CARTESIAN_POINT('Ctrl Pts',(-18.9043261767328,-16.8406111195394,
0.1006127503883));
#159097=CARTESIAN_POINT('Ctrl Pts',(-18.8317055633233,-16.8372558965928,
0.104989018218294));
#159098=CARTESIAN_POINT('Ctrl Pts',(-18.7589608117345,-16.8338949382048,
0.109372766870811));
#159099=CARTESIAN_POINT('Ctrl Pts',(-18.6861364519365,-16.8342961174985,
0.113756515523328));
#159100=CARTESIAN_POINT('Ctrl Pts',(-18.6136477260043,-16.8384238054558,
0.118140264175844));
#159101=CARTESIAN_POINT('Ctrl Pts',(-18.5716413935222,-16.8408157502787,
0.120680593048329));
#159102=CARTESIAN_POINT('Ctrl Pts',(-18.5297476644012,-16.8444581093918,
0.123220921920813));
#159103=CARTESIAN_POINT('Ctrl Pts',(-18.4880458342194,-16.8493360828855,
0.125761250793297));
#159104=CARTESIAN_POINT('Ctrl Pts',(-18.4158851594457,-16.8577769080795,
0.13015702538607));
#159105=CARTESIAN_POINT('Ctrl Pts',(-18.3440241643562,-16.8699525372844,
0.134552799978843));
#159106=CARTESIAN_POINT('Ctrl Pts',(-18.2728786958473,-16.8858305628878,
0.138948574571615));
#159107=CARTESIAN_POINT('Ctrl Pts',(-18.2018360533927,-16.9016856400904,
0.143337995981724));
#159108=CARTESIAN_POINT('Ctrl Pts',(-18.1315073495764,-16.9212323858817,
0.147727417391832));
#159109=CARTESIAN_POINT('Ctrl Pts',(-18.0623020683668,-16.9443867681648,
0.152116838801941));
#159110=CARTESIAN_POINT('Ctrl Pts',(-17.9931748039694,-16.9675150479445,
0.156501311909549));
#159111=CARTESIAN_POINT('Ctrl Pts',(-17.9251688996744,-16.9942427328982,
0.160885785017158));
#159112=CARTESIAN_POINT('Ctrl Pts',(-17.8586807914585,-17.0244354010414,
0.165270258124766));
#159113=CARTESIAN_POINT('Ctrl Pts',(-17.79223296666,-17.0546097762314,0.16965207479403));
#159114=CARTESIAN_POINT('Ctrl Pts',(-17.7273015495519,-17.0882447704819,
0.174033891463294));
#159115=CARTESIAN_POINT('Ctrl Pts',(-17.6642636992251,-17.1251575747196,
0.178415708132558));
#159116=CARTESIAN_POINT('Ctrl Pts',(-17.6012434550811,-17.1620600693801,
0.182796300980494));
#159117=CARTESIAN_POINT('Ctrl Pts',(-17.5401161419553,-17.2022383136031,
0.18717689382843));
#159118=CARTESIAN_POINT('Ctrl Pts',(-17.481233502117,-17.2454640051314,
0.191557486676366));
#159119=CARTESIAN_POINT('Ctrl Pts',(-17.4223480788122,-17.2886917400001,
0.19593828660119));
#159120=CARTESIAN_POINT('Ctrl Pts',(-17.3657079255823,-17.3349669223205,
0.200319086526014));
#159121=CARTESIAN_POINT('Ctrl Pts',(-17.3116336689764,-17.3840194451555,
0.204699886450838));
#159122=CARTESIAN_POINT('Ctrl Pts',(-17.2575022929462,-17.4331237828844,
0.20908531387839));
#159123=CARTESIAN_POINT('Ctrl Pts',(-17.2059425814251,-17.4850109948883,
0.213470741305941));
#159124=CARTESIAN_POINT('Ctrl Pts',(-17.1572394598231,-17.5393729441424,
0.217856168733493));
#159125=CARTESIAN_POINT('Ctrl Pts',(-17.1085090930288,-17.5937653042144,
0.222244049429123));
#159126=CARTESIAN_POINT('Ctrl Pts',(-17.0626387997765,-17.6506347838424,
0.226631930124754));
#159127=CARTESIAN_POINT('Ctrl Pts',(-17.019872504564,-17.7096409820868,
0.231019810820385));
#159128=CARTESIAN_POINT('Ctrl Pts',(-16.9770304728485,-17.7687516767129,
0.23541546218537));
#159129=CARTESIAN_POINT('Ctrl Pts',(-16.9373036781403,-17.8300062430902,
0.239811113550356));
#159130=CARTESIAN_POINT('Ctrl Pts',(-16.9008917879239,-17.8930366942999,
0.244206764915342));
#159131=CARTESIAN_POINT('Ctrl Pts',(-16.8767856560651,-17.9347653812468,
0.247116862435138));
#159132=CARTESIAN_POINT('Ctrl Pts',(-16.8541314891368,-17.9772719122011,
0.250026959954935));
#159133=CARTESIAN_POINT('Ctrl Pts',(-16.8329756005513,-18.0204447237547,
0.252937057474732));
#159134=CARTESIAN_POINT('Ctrl Pts',(-16.8011149915786,-18.0854626529992,
0.257319642435692));
#159135=CARTESIAN_POINT('Ctrl Pts',(-16.7725300877984,-18.1522470560442,
0.261702227396652));
#159136=CARTESIAN_POINT('Ctrl Pts',(-16.7474199512368,-18.2204340700553,
0.266084812357612));
#159137=CARTESIAN_POINT('Ctrl Pts',(-16.7223475943392,-18.2885184927293,
0.270460803464049));
#159138=CARTESIAN_POINT('Ctrl Pts',(-16.7007397931117,-18.3580008874103,
0.274836794570485));
#159139=CARTESIAN_POINT('Ctrl Pts',(-16.6827489310325,-18.4284944584252,
0.279212785676921));
#159140=CARTESIAN_POINT('Ctrl Pts',(-16.6647796228869,-18.4989035746903,
0.283583534131738));
#159141=CARTESIAN_POINT('Ctrl Pts',(-16.6504187653927,-18.5703209945558,
0.287954282586556));
#159142=CARTESIAN_POINT('Ctrl Pts',(-16.6397694152316,-18.6423433226608,
0.292325031041373));
#159143=CARTESIAN_POINT('Ctrl Pts',(-16.6291269614596,-18.714319009986,
0.29669294905288));
#159144=CARTESIAN_POINT('Ctrl Pts',(-16.6221913171743,-18.7868983510167,
0.301060867064387));
#159145=CARTESIAN_POINT('Ctrl Pts',(-16.6190144817355,-18.8596676788374,
0.305428785075894));
#159146=CARTESIAN_POINT('Ctrl Pts',(-16.6158386481743,-18.9324140574164,
0.309795325578371));
#159147=CARTESIAN_POINT('Ctrl Pts',(-16.616419291388,-19.0053498208129,
0.314161866080847));
#159148=CARTESIAN_POINT('Ctrl Pts',(-16.6207564193529,-19.0780577996553,
0.318528406583324));
#159149=CARTESIAN_POINT('Ctrl Pts',(-16.6250936203624,-19.1507670030232,
0.322895020625736));
#159150=CARTESIAN_POINT('Ctrl Pts',(-16.6331874009118,-19.2232479313927,
0.327261634668148));
#159151=CARTESIAN_POINT('Ctrl Pts',(-16.6449857626134,-19.2950867470421,
0.33162824871056));
#159152=CARTESIAN_POINT('Ctrl Pts',(-16.6567963363639,-19.3669999203992,
0.335999382474067));
#159153=CARTESIAN_POINT('Ctrl Pts',(-16.6723190685484,-19.4382691756095,
0.340370516237575));
#159154=CARTESIAN_POINT('Ctrl Pts',(-16.6914506293117,-19.5084899534592,
0.344741650001082));
#159155=CARTESIAN_POINT('Ctrl Pts',(-16.7105925668403,-19.578748818349,
0.349115154623362));
#159156=CARTESIAN_POINT('Ctrl Pts',(-16.7333470785608,-19.6479576138078,
0.353488659245642));
#159157=CARTESIAN_POINT('Ctrl Pts',(-16.7595614725531,-19.7157286830631,
0.357862163867922));
#159158=CARTESIAN_POINT('Ctrl Pts',(-16.7858226024992,-19.7836205769906,
0.362243465729771));
#159159=CARTESIAN_POINT('Ctrl Pts',(-16.8155557348011,-19.8500691841256,
0.36662476759162));
#159160=CARTESIAN_POINT('Ctrl Pts',(-16.8485609817509,-19.9147090466303,
0.371006069453469));
#159161=CARTESIAN_POINT('Ctrl Pts',(-16.871428766834,-19.9594949706928,
0.374041667687701));
#159162=CARTESIAN_POINT('Ctrl Pts',(-16.8958663395961,-20.0034131234881,
0.377077265921934));
#159163=CARTESIAN_POINT('Ctrl Pts',(-16.9217951774031,-20.0463503465328,
0.380112864156166));
#159164=CARTESIAN_POINT('Ctrl Pts',(-16.9592871194148,-20.108435654348,
0.384502203694482));
#159165=CARTESIAN_POINT('Ctrl Pts',(-17.0000462087351,-20.1687128298791,
0.388891543232798));
#159166=CARTESIAN_POINT('Ctrl Pts',(-17.0438726579669,-20.2268170722547,
0.393280882771114));
#159167=CARTESIAN_POINT('Ctrl Pts',(-17.0876341208282,-20.2848351569816,
0.397663713745537));
#159168=CARTESIAN_POINT('Ctrl Pts',(-17.1344536264988,-20.3406863231545,
0.402046544719961));
#159169=CARTESIAN_POINT('Ctrl Pts',(-17.1840869213948,-20.3940327488544,
0.406429375694384));
#159170=CARTESIAN_POINT('Ctrl Pts',(-17.2336619167729,-20.4473165135743,
0.410807058573494));
#159171=CARTESIAN_POINT('Ctrl Pts',(-17.2860438089119,-20.4981010311794,
0.415184741452605));
#159172=CARTESIAN_POINT('Ctrl Pts',(-17.3409477702607,-20.5460810786213,
0.419562424331716));
#159173=CARTESIAN_POINT('Ctrl Pts',(-17.3958169194766,-20.5940307040727,
0.42393733151897));
#159174=CARTESIAN_POINT('Ctrl Pts',(-17.4532046028361,-20.6391790711337,
0.428312238706224));
#159175=CARTESIAN_POINT('Ctrl Pts',(-17.5127898056829,-20.6812584136837,
0.432687145893477));
#159176=CARTESIAN_POINT('Ctrl Pts',(-17.5723568562232,-20.723324936992,
0.437060720289165));
#159177=CARTESIAN_POINT('Ctrl Pts',(-17.6341197035787,-20.7623240140802,
0.441434294684853));
#159178=CARTESIAN_POINT('Ctrl Pts',(-17.6977263244876,-20.7980297585467,
0.445807869080541));
#159179=CARTESIAN_POINT('Ctrl Pts',(-17.7613345200931,-20.8337363869733,
0.450181551751944));
#159180=CARTESIAN_POINT('Ctrl Pts',(-17.8267861585152,-20.8661492866597,
0.454555234423347));
#159181=CARTESIAN_POINT('Ctrl Pts',(-17.8937039331709,-20.8950881400676,
0.45892891709475));
#159182=CARTESIAN_POINT('Ctrl Pts',(-17.9606909349872,-20.924056931032,
0.463307124388118));
#159183=CARTESIAN_POINT('Ctrl Pts',(-18.0291466578795,-20.9495443083807,
0.467685331681485));
#159184=CARTESIAN_POINT('Ctrl Pts',(-18.0986738647242,-20.9714181592319,
0.472063538974852));
#159185=CARTESIAN_POINT('Ctrl Pts',(-18.1682389417348,-20.9933039243595,
0.476444130995642));
#159186=CARTESIAN_POINT('Ctrl Pts',(-18.2388761976446,-21.0115721233672,
0.480824723016432));
#159187=CARTESIAN_POINT('Ctrl Pts',(-18.3101759171462,-21.0261413034779,
0.485205315037221));
#159188=CARTESIAN_POINT('Ctrl Pts',(-18.3816016288558,-21.040736228475,
0.48959364790839));
#159189=CARTESIAN_POINT('Ctrl Pts',(-18.453691664747,-21.0516190094181,
0.49398198077956));
#159190=CARTESIAN_POINT('Ctrl Pts',(-18.5260294507966,-21.0587598939281,
0.498370313650729));
#159191=CARTESIAN_POINT('Ctrl Pts',(-18.5750331942104,-21.063597339078,
0.501343099379686));
#159192=CARTESIAN_POINT('Ctrl Pts',(-18.6241505410345,-21.0667186770647,
0.504315885108644));
#159193=CARTESIAN_POINT('Ctrl Pts',(-18.6732524746729,-21.0681282423725,
0.507288670837601));
#159194=CARTESIAN_POINT('Ctrl Pts',(-18.7457477477536,-21.0702093584171,
0.511677763023228));
#159195=CARTESIAN_POINT('Ctrl Pts',(-18.8184909227825,-21.068564845846,
0.516066855208855));
#159196=CARTESIAN_POINT('Ctrl Pts',(-18.8910671418926,-21.063165297398,
0.520455947394481));
#159197=CARTESIAN_POINT('Ctrl Pts',(-18.9635359951035,-21.0577737367921,
0.524838546560292));
#159198=CARTESIAN_POINT('Ctrl Pts',(-19.035837905828,-21.0486382034475,
0.529221145726103));
#159199=CARTESIAN_POINT('Ctrl Pts',(-19.1075566421874,-21.0357812829272,
0.533603744891914));
#159200=CARTESIAN_POINT('Ctrl Pts',(-19.1791915341236,-21.0229393930828,
0.537981220480296));
#159201=CARTESIAN_POINT('Ctrl Pts',(-19.2502441338016,-21.0063848432238,
0.542358696068678));
#159202=CARTESIAN_POINT('Ctrl Pts',(-19.32030366582,-20.9861919799876,0.54673617165706));
#159203=CARTESIAN_POINT('Ctrl Pts',(-19.3903190177729,-20.9660118505222,
0.551110886776558));
#159204=CARTESIAN_POINT('Ctrl Pts',(-19.4593420824552,-20.9421980932421,
0.555485601896056));
#159205=CARTESIAN_POINT('Ctrl Pts',(-19.5269740036053,-20.91487575501,0.559860317015555));
#159206=CARTESIAN_POINT('Ctrl Pts',(-19.594585560535,-20.8875616436346,
0.564233714892226));
#159207=CARTESIAN_POINT('Ctrl Pts',(-19.6608063587658,-20.8567412292126,
0.568607112768897));
#159208=CARTESIAN_POINT('Ctrl Pts',(-19.7252559833366,-20.8225882966327,
0.572980510645567));
#159209=CARTESIAN_POINT('Ctrl Pts',(-19.7897074377077,-20.7884343944112,
0.577354032688118));
#159210=CARTESIAN_POINT('Ctrl Pts',(-19.852387193486,-20.7509480137079,
0.581727554730669));
#159211=CARTESIAN_POINT('Ctrl Pts',(-19.9129394779501,-20.7103488582562,
0.58610107677322));
#159212=CARTESIAN_POINT('Ctrl Pts',(-19.9735547637542,-20.6697074616038,
0.590479149226244));
#159213=CARTESIAN_POINT('Ctrl Pts',(-20.0320377575059,-20.6259470930867,
0.594857221679268));
#159214=CARTESIAN_POINT('Ctrl Pts',(-20.0880624400643,-20.5793303009552,
0.599235294132292));
#159215=CARTESIAN_POINT('Ctrl Pts',(-20.1441178212582,-20.5326879652269,
0.603615765543133));
#159216=CARTESIAN_POINT('Ctrl Pts',(-20.1977118548978,-20.4831864169906,
0.607996236953973));
#159217=CARTESIAN_POINT('Ctrl Pts',(-20.2485543758915,-20.431126107696,
0.612376708364814));
#159218=CARTESIAN_POINT('Ctrl Pts',(-20.2994870261129,-20.3789735103839,
0.616764945096839));
#159219=CARTESIAN_POINT('Ctrl Pts',(-20.3476581043648,-20.3242534561182,
0.621153181828863));
#159220=CARTESIAN_POINT('Ctrl Pts',(-20.3928172134662,-20.2673001377284,
0.625541418560888));
#159221=CARTESIAN_POINT('Ctrl Pts',(-20.4234261206892,-20.2286970989766,
0.628515771546937));
#159222=CARTESIAN_POINT('Ctrl Pts',(-20.4526521510532,-20.189068732231,
0.631490124532986));
#159223=CARTESIAN_POINT('Ctrl Pts',(-20.4804290435443,-20.1485260531492,
0.634464477519035));
#159224=CARTESIAN_POINT('Ctrl Pts',(-20.5219871713971,-20.0878685177061,
0.638914526843781));
#159225=CARTESIAN_POINT('Ctrl Pts',(-20.5604589871816,-20.0249304539103,
0.643364576168526));
#159226=CARTESIAN_POINT('Ctrl Pts',(-20.5955899081637,-19.9600535768614,
0.647814625493272));
#159227=CARTESIAN_POINT('Ctrl Pts',(-20.6306645362352,-19.8952806569004,
0.652257544170088));
#159228=CARTESIAN_POINT('Ctrl Pts',(-20.6624086819058,-19.8285754984249,
0.656700462846903));
#159229=CARTESIAN_POINT('Ctrl Pts',(-20.6906106771651,-19.7603091351726,
0.661143381523719));
#159230=CARTESIAN_POINT('Ctrl Pts',(-20.7187693668652,-19.6921475982991,
0.665579477879059));
#159231=CARTESIAN_POINT('Ctrl Pts',(-20.7433965459121,-19.6224300506977,
0.670015574234399));
#159232=CARTESIAN_POINT('Ctrl Pts',(-20.7643269859574,-19.5515509403655,
0.674451670589739));
#159233=CARTESIAN_POINT('Ctrl Pts',(-20.7852384369126,-19.4807361349314,
0.678883742307599));
#159234=CARTESIAN_POINT('Ctrl Pts',(-20.8024596788638,-19.4087623035746,
0.683315814025459));
#159235=CARTESIAN_POINT('Ctrl Pts',(-20.8158743946738,-19.3360416706575,
0.687747885743319));
#159236=CARTESIAN_POINT('Ctrl Pts',(-20.8292815682241,-19.2633619240265,
0.692177465583092));
#159237=CARTESIAN_POINT('Ctrl Pts',(-20.8388863810041,-19.1899366656731,
0.696607045422866));
#159238=CARTESIAN_POINT('Ctrl Pts',(-20.8446233100443,-19.1161896558795,
0.70103662526264));
#159239=CARTESIAN_POINT('Ctrl Pts',(-20.8489003376003,-19.0612093709814,
0.704338990500929));
#159240=CARTESIAN_POINT('Ctrl Pts',(-20.8510286073489,-19.0060505461427,
0.707641355739218));
#159241=CARTESIAN_POINT('Ctrl Pts',(-20.8509997094775,-18.950890913829,
0.710943720977507));
#159242=CARTESIAN_POINT('',(-17.1140743056112,-17.5890877707427,0.));
#159243=CARTESIAN_POINT('Origin',(-18.734,-18.952,0.));
#159244=CARTESIAN_POINT('',(-20.8509993841888,-18.9503852727442,0.489056278967187));
#159245=CARTESIAN_POINT('Ctrl Pts',(-20.8509993841888,-18.9503852727442,
0.489056278967187));
#159246=CARTESIAN_POINT('Ctrl Pts',(-20.8510560136238,-19.0246296868351,
0.4845759098454));
#159247=CARTESIAN_POINT('Ctrl Pts',(-20.8472020786515,-19.0990185847436,
0.480095540723613));
#159248=CARTESIAN_POINT('Ctrl Pts',(-20.8394225353484,-19.1730994067089,
0.475615171601827));
#159249=CARTESIAN_POINT('Ctrl Pts',(-20.8319236706916,-19.2445074619042,
0.471296450007534));
#159250=CARTESIAN_POINT('Ctrl Pts',(-20.8207776586562,-19.315628743596,
0.466977728413241));
#159251=CARTESIAN_POINT('Ctrl Pts',(-20.8060239434695,-19.3860573437798,
0.462659006818948));
#159252=CARTESIAN_POINT('Ctrl Pts',(-20.7912800569942,-19.4564390254502,
0.458343162294427));
#159253=CARTESIAN_POINT('Ctrl Pts',(-20.7729333335852,-19.5261284557063,
0.454027317769906));
#159254=CARTESIAN_POINT('Ctrl Pts',(-20.7510747167063,-19.5947274595226,
0.449711473245385));
#159255=CARTESIAN_POINT('Ctrl Pts',(-20.729222990825,-19.6633048372874,
0.445396989304411));
#159256=CARTESIAN_POINT('Ctrl Pts',(-20.703861718916,-19.7307919977793,
0.441082505363437));
#159257=CARTESIAN_POINT('Ctrl Pts',(-20.6751318649418,-19.7968053520828,
0.436768021422464));
#159258=CARTESIAN_POINT('Ctrl Pts',(-20.6464009865417,-19.8628210602368,
0.43245338363913));
#159259=CARTESIAN_POINT('Ctrl Pts',(-20.6143014889206,-19.9273624038596,
0.428138745855796));
#159260=CARTESIAN_POINT('Ctrl Pts',(-20.5790219450864,-19.9900669641933,
0.423824108072462));
#159261=CARTESIAN_POINT('Ctrl Pts',(-20.5437075127064,-20.052833534142,
0.419505203469831));
#159262=CARTESIAN_POINT('Ctrl Pts',(-20.5052070056352,-20.1137592644334,
0.4151862988672));
#159263=CARTESIAN_POINT('Ctrl Pts',(-20.4637537424931,-20.1725084966239,
0.410867394264568));
#159264=CARTESIAN_POINT('Ctrl Pts',(-20.4222758241251,-20.2312926711924,
0.406545920899905));
#159265=CARTESIAN_POINT('Ctrl Pts',(-20.377841965069,-20.2878973842407,
0.402224447535242));
#159266=CARTESIAN_POINT('Ctrl Pts',(-20.3307256528942,-20.3420202118637,
0.397902974170579));
#159267=CARTESIAN_POINT('Ctrl Pts',(-20.2835347523397,-20.3962287196649,
0.393574659614792));
#159268=CARTESIAN_POINT('Ctrl Pts',(-20.2336532763038,-20.4479471527698,
0.389246345059005));
#159269=CARTESIAN_POINT('Ctrl Pts',(-20.1813905761972,-20.4969108453033,
0.384918030503218));
#159270=CARTESIAN_POINT('Ctrl Pts',(-20.1677438125197,-20.5096961767043,
0.383787827016913));
#159271=CARTESIAN_POINT('Ctrl Pts',(-20.153934855464,-20.5222939030973,
0.382657623530608));
#159272=CARTESIAN_POINT('Ctrl Pts',(-20.1399695482849,-20.534699791273,
0.381527420044303));
#159273=CARTESIAN_POINT('Ctrl Pts',(-20.0856805306588,-20.5829266919206,
0.37713384414925));
#159274=CARTESIAN_POINT('Ctrl Pts',(-20.0288042210984,-20.628448612849,
0.372740268254198));
#159275=CARTESIAN_POINT('Ctrl Pts',(-19.9696409341315,-20.6709765797994,
0.368346692359146));
#159276=CARTESIAN_POINT('Ctrl Pts',(-19.9105639454999,-20.7134425134696,
0.363959525139228));
#159277=CARTESIAN_POINT('Ctrl Pts',(-19.8492069897093,-20.7529228848839,
0.359572357919309));
#159278=CARTESIAN_POINT('Ctrl Pts',(-19.7859047362902,-20.7891677728967,
0.355185190699391));
#159279=CARTESIAN_POINT('Ctrl Pts',(-19.7226749495449,-20.8253711687614,
0.350803045787509));
#159280=CARTESIAN_POINT('Ctrl Pts',(-19.6575047045699,-20.8583462016275,
0.346420900875626));
#159281=CARTESIAN_POINT('Ctrl Pts',(-19.5907576513136,-20.8878861864571,
0.342038755963743));
#159282=CARTESIAN_POINT('Ctrl Pts',(-19.5240517390544,-20.9174079636751,
0.337659312082127));
#159283=CARTESIAN_POINT('Ctrl Pts',(-19.4557713858206,-20.9434987000513,
0.333279868200511));
#159284=CARTESIAN_POINT('Ctrl Pts',(-19.3863035870799,-20.9659982696822,
0.328900424318895));
#159285=CARTESIAN_POINT('Ctrl Pts',(-19.3168558633837,-20.9884913373096,
0.324522246024112));
#159286=CARTESIAN_POINT('Ctrl Pts',(-19.2462218327664,-21.0073951506619,
0.320144067729329));
#159287=CARTESIAN_POINT('Ctrl Pts',(-19.1748055877231,-21.0225988104488,
0.315765889434546));
#159288=CARTESIAN_POINT('Ctrl Pts',(-19.1033866007396,-21.0378030539619,
0.311387543044908));
#159289=CARTESIAN_POINT('Ctrl Pts',(-19.0311858104647,-21.0493067636484,
0.307009196655271));
#159290=CARTESIAN_POINT('Ctrl Pts',(-18.9586178566869,-21.0570500750475,
0.302630850265634));
#159291=CARTESIAN_POINT('Ctrl Pts',(-18.8859739522814,-21.0648014907037,
0.298247921437894));
#159292=CARTESIAN_POINT('Ctrl Pts',(-18.8129625963384,-21.0687845992062,
0.293864992610155));
#159293=CARTESIAN_POINT('Ctrl Pts',(-18.7400030989875,-21.0689914885995,
0.289482063782416));
#159294=CARTESIAN_POINT('Ctrl Pts',(-18.6670032476659,-21.0691984924235,
0.285096710752373));
#159295=CARTESIAN_POINT('Ctrl Pts',(-18.5940557926885,-21.0656251419751,
0.280711357722329));
#159296=CARTESIAN_POINT('Ctrl Pts',(-18.5215768813658,-21.0583156028169,
0.276326004692286));
#159297=CARTESIAN_POINT('Ctrl Pts',(-18.4489698822543,-21.0509931459328,
0.271932901681422));
#159298=CARTESIAN_POINT('Ctrl Pts',(-18.3768335560972,-21.039921387774,
0.267539798670557));
#159299=CARTESIAN_POINT('Ctrl Pts',(-18.3055752234049,-21.0251958930114,
0.263146695659693));
#159300=CARTESIAN_POINT('Ctrl Pts',(-18.258021675733,-21.0153689788707,
0.260215001560752));
#159301=CARTESIAN_POINT('Ctrl Pts',(-18.2108588965979,-21.0039159582902,
0.25728330746181));
#159302=CARTESIAN_POINT('Ctrl Pts',(-18.164203666426,-20.9908774210937,
0.254351613362869));
#159303=CARTESIAN_POINT('Ctrl Pts',(-18.0951064200439,-20.9715671098208,
0.250009720959284));
#159304=CARTESIAN_POINT('Ctrl Pts',(-18.0268407868783,-20.9486978630522,
0.245667828555699));
#159305=CARTESIAN_POINT('Ctrl Pts',(-17.9598054524231,-20.922358292926,
0.241325936152114));
#159306=CARTESIAN_POINT('Ctrl Pts',(-17.8928710627946,-20.8960583861112,
0.236990581965715));
#159307=CARTESIAN_POINT('Ctrl Pts',(-17.8271637514137,-20.8662987014601,
0.232655227779317));
#159308=CARTESIAN_POINT('Ctrl Pts',(-17.763068724128,-20.8332180781434,
0.228319873592918));
#159309=CARTESIAN_POINT('Ctrl Pts',(-17.699047363678,-20.8001754756366,
0.223989502192827));
#159310=CARTESIAN_POINT('Ctrl Pts',(-17.6366350451716,-20.7638197356247,
0.219659130792735));
#159311=CARTESIAN_POINT('Ctrl Pts',(-17.5761969042586,-20.7243377193672,
0.215328759392644));
#159312=CARTESIAN_POINT('Ctrl Pts',(-17.5157959073165,-20.6848799679007,
0.211001049344912));
#159313=CARTESIAN_POINT('Ctrl Pts',(-17.457367094634,-20.6423000184136,
0.206673339297181));
#159314=CARTESIAN_POINT('Ctrl Pts',(-17.4012494835622,-20.5968297969501,
0.202345629249449));
#159315=CARTESIAN_POINT('Ctrl Pts',(-17.3451469193491,-20.5513717674523,
0.198019079593976));
#159316=CARTESIAN_POINT('Ctrl Pts',(-17.2913547105839,-20.5030253137849,
0.193692529938503));
#159317=CARTESIAN_POINT('Ctrl Pts',(-17.2401799611388,-20.4520635624855,
0.18936598028303));
#159318=CARTESIAN_POINT('Ctrl Pts',(-17.1890012037485,-20.4010978199226,
0.185039091777358));
#159319=CARTESIAN_POINT('Ctrl Pts',(-17.1404406606225,-20.3475167229364,
0.180712203271685));
#159320=CARTESIAN_POINT('Ctrl Pts',(-17.0947683110377,-20.2916299749938,
0.176385314766013));
#159321=CARTESIAN_POINT('Ctrl Pts',(-17.0490411502534,-20.2356761575941,
0.172053233579186));
#159322=CARTESIAN_POINT('Ctrl Pts',(-17.0062094147358,-20.1774115489121,
0.167721152392358));
#159323=CARTESIAN_POINT('Ctrl Pts',(-16.9665019464716,-20.1171779395326,
0.16338907120553));
#159324=CARTESIAN_POINT('Ctrl Pts',(-16.9267699714228,-20.0569071549778,
0.159054316330717));
#159325=CARTESIAN_POINT('Ctrl Pts',(-16.8901663478009,-19.9946653786934,
0.154719561455904));
#159326=CARTESIAN_POINT('Ctrl Pts',(-16.8568742859376,-19.9308197247736,
0.150384806581091));
#159327=CARTESIAN_POINT('Ctrl Pts',(-16.8235151748393,-19.8668454875814,
0.146041321637236));
#159328=CARTESIAN_POINT('Ctrl Pts',(-16.793481145719,-19.8012613727176,
0.141697836693382));
#159329=CARTESIAN_POINT('Ctrl Pts',(-16.7669073048299,-19.7344546815047,
0.137354351749528));
#159330=CARTESIAN_POINT('Ctrl Pts',(-16.7461495461317,-19.6822696330047,
0.133961503393496));
#159331=CARTESIAN_POINT('Ctrl Pts',(-16.7275021235515,-19.6293390357121,
0.130568655037465));
#159332=CARTESIAN_POINT('Ctrl Pts',(-16.7110078198973,-19.5758522575445,
0.127175806681434));
#159333=CARTESIAN_POINT('Ctrl Pts',(-16.6890805816263,-19.5047478718232,
0.122665413525099));
#159334=CARTESIAN_POINT('Ctrl Pts',(-16.670871275646,-19.4323727566685,
0.118155020368764));
#159335=CARTESIAN_POINT('Ctrl Pts',(-16.6565191765188,-19.3591393226743,
0.113644627212429));
#159336=CARTESIAN_POINT('Ctrl Pts',(-16.641451763523,-19.2822559075513,
0.108909434411911));
#159337=CARTESIAN_POINT('Ctrl Pts',(-16.6306362897029,-19.2044268305763,
0.104174241611394));
#159338=CARTESIAN_POINT('Ctrl Pts',(-16.6241750766647,-19.1261487664996,
0.0994390488108757));
#159339=CARTESIAN_POINT('Ctrl Pts',(-16.618041066305,-19.0518347865785,
0.0949436511940506));
#159340=CARTESIAN_POINT('Ctrl Pts',(-16.6158311203138,-18.9771167035359,
0.0904482535772255));
#159341=CARTESIAN_POINT('Ctrl Pts',(-16.6175804393308,-18.9024294117756,
0.0859528559604003));
#159342=CARTESIAN_POINT('Ctrl Pts',(-16.6193281134804,-18.8278123477383,
0.0814616853215709));
#159343=CARTESIAN_POINT('Ctrl Pts',(-16.6250276422425,-18.7532264655291,
0.0769705146827415));
#159344=CARTESIAN_POINT('Ctrl Pts',(-16.6346622154624,-18.6791083247648,
0.0724793440439121));
#159345=CARTESIAN_POINT('Ctrl Pts',(-16.6442902465126,-18.6050405124837,
0.0679912230472238));
#159346=CARTESIAN_POINT('Ctrl Pts',(-16.6578479512151,-18.5314402553688,
0.0635031020505355));
#159347=CARTESIAN_POINT('Ctrl Pts',(-16.6752666606882,-18.458739381659,
0.0590149810538472));
#159348=CARTESIAN_POINT('Ctrl Pts',(-16.6926780888339,-18.3860688981953,
0.0545287361708016));
#159349=CARTESIAN_POINT('Ctrl Pts',(-16.7139472060124,-18.3142974872696,
0.0500424912877559));
#159350=CARTESIAN_POINT('Ctrl Pts',(-16.738954437569,-18.2438459180203,
0.0455562464047103));
#159351=CARTESIAN_POINT('Ctrl Pts',(-16.7639647762088,-18.1733855953477,
0.0410694441174684));
#159352=CARTESIAN_POINT('Ctrl Pts',(-16.7927140135935,-18.1042458686283,
0.0365826418302264));
#159353=CARTESIAN_POINT('Ctrl Pts',(-16.8250332584604,-18.0368306278641,
0.0320958395429845));
#159354=CARTESIAN_POINT('Ctrl Pts',(-16.8573540573157,-17.9694121456102,
0.0276088215193051));
#159355=CARTESIAN_POINT('Ctrl Pts',(-16.893245003916,-17.9037187169574,
0.0231218034956257));
#159356=CARTESIAN_POINT('Ctrl Pts',(-16.9324905209222,-17.8401310343422,
0.0186347854719464));
#159357=CARTESIAN_POINT('Ctrl Pts',(-16.971763121732,-17.776499469102,0.0141446709031355));
#159358=CARTESIAN_POINT('Ctrl Pts',(-17.0143946720501,-17.7149769304511,
0.00965455633432465));
#159359=CARTESIAN_POINT('Ctrl Pts',(-17.0601258387639,-17.65591578501,0.00516444176551379));
#159360=CARTESIAN_POINT('Ctrl Pts',(-17.0776588692871,-17.6332721277373,
0.00344296117700913));
#159361=CARTESIAN_POINT('Ctrl Pts',(-17.0956470822643,-17.6109899387145,
0.00172148058850446));
#159362=CARTESIAN_POINT('Ctrl Pts',(-17.1140743056112,-17.5890877707427,
-2.02192933296002E-16));
#159363=CARTESIAN_POINT('Ctrl Pts',(-20.8509994311265,-18.9504480302426,
0.490010487033197));
#159364=CARTESIAN_POINT('Ctrl Pts',(-20.8509485264066,-18.8810102963088,
0.494577353552967));
#159365=CARTESIAN_POINT('Ctrl Pts',(-20.8474812861683,-18.8116101392654,
0.499099022991477));
#159366=CARTESIAN_POINT('Ctrl Pts',(-20.8382974724733,-18.7192631654625,
0.504962284114916));
#159367=CARTESIAN_POINT('Ctrl Pts',(-20.835602182128,-18.6960651320075,
0.506421988151869));
#159368=CARTESIAN_POINT('Ctrl Pts',(-20.831714710083,-18.6668340267685,
0.508240727451452));
#159369=CARTESIAN_POINT('Ctrl Pts',(-20.8308795002837,-18.6607561149905,
0.508617762711525));
#159370=CARTESIAN_POINT('Ctrl Pts',(-20.8294396311101,-18.6506054014144,
0.509245465875726));
#159371=CARTESIAN_POINT('Ctrl Pts',(-20.8288494962058,-18.6465306225147,
0.509496908631013));
#159372=CARTESIAN_POINT('Ctrl Pts',(-20.8277537529322,-18.6391172367348,
0.509953361381631));
#159373=CARTESIAN_POINT('Ctrl Pts',(-20.8272520391161,-18.6357780801865,
0.510158586227083));
#159374=CARTESIAN_POINT('Ctrl Pts',(-20.8262054025295,-18.6289238385501,
0.510579064774858));
#159375=CARTESIAN_POINT('Ctrl Pts',(-20.8256596119141,-18.6254089394044,
0.510794262175057));
#159376=CARTESIAN_POINT('Ctrl Pts',(-20.8244066763097,-18.6174720023468,
0.511279232147259));
#159377=CARTESIAN_POINT('Ctrl Pts',(-20.8236943601969,-18.6130508365728,
0.511548707398385));
#159378=CARTESIAN_POINT('Ctrl Pts',(-20.821498981492,-18.5996946857722,
0.512360842528697));
#159379=CARTESIAN_POINT('Ctrl Pts',(-20.8199725808866,-18.590766791922,
0.512901088674201));
#159380=CARTESIAN_POINT('Ctrl Pts',(-20.8078179693633,-18.5223219602975,
0.517024578341899));
#159381=CARTESIAN_POINT('Ctrl Pts',(-20.7947008199896,-18.4632692387237,
0.520476395378648));
#159382=CARTESIAN_POINT('Ctrl Pts',(-20.7741834180103,-18.3865812121723,
0.524914225206502));
#159383=CARTESIAN_POINT('Ctrl Pts',(-20.7690499488155,-18.3683746774345,
0.525964408236979));
#159384=CARTESIAN_POINT('Ctrl Pts',(-20.7520366525769,-18.3109907112767,
0.52927032329694));
#159385=CARTESIAN_POINT('Ctrl Pts',(-20.7392639646607,-18.2720871905213,
0.53150561845119));
#159386=CARTESIAN_POINT('Ctrl Pts',(-20.7244457869367,-18.231013174881,
0.533880934072488));
#159387=CARTESIAN_POINT('Ctrl Pts',(-20.7235156490763,-18.2284504754409,
0.534029198950805));
#159388=CARTESIAN_POINT('Ctrl Pts',(-20.7225805737341,-18.2258896077265,
0.534177427254548));
#159389=CARTESIAN_POINT('Origin',(-18.734,-18.952,0.));
#159390=CARTESIAN_POINT('',(-20.7225805817976,-18.2258896298098,1.55576077259463));
#159391=CARTESIAN_POINT('',(-20.7225805737606,-18.2258896077991,1.33163200235201));
#159392=CARTESIAN_POINT('',(-20.7225805737622,-18.2258896078036,0.));
#159393=CARTESIAN_POINT('',(-20.8509996091575,-18.9507135992268,1.51094372094299));
#159394=CARTESIAN_POINT('Ctrl Pts',(-20.7225805817976,-18.2258896298098,
1.55576077259462));
#159395=CARTESIAN_POINT('Ctrl Pts',(-20.7518710589646,-18.3061067380035,
1.55012867077602));
#159396=CARTESIAN_POINT('Ctrl Pts',(-20.7762853815704,-18.38803479713,1.54445865839829));
#159397=CARTESIAN_POINT('Ctrl Pts',(-20.8019773168351,-18.4982088405443,
1.53708130683603));
#159398=CARTESIAN_POINT('Ctrl Pts',(-20.8077392211968,-18.5253123572864,
1.53528617643754));
#159399=CARTESIAN_POINT('Ctrl Pts',(-20.8211288647775,-18.5949948853297,
1.53073317031627));
#159400=CARTESIAN_POINT('Ctrl Pts',(-20.8279872923736,-18.6377113451497,
1.52800101026692));
#159401=CARTESIAN_POINT('Ctrl Pts',(-20.8344943172588,-18.6880513212877,
1.52487280887383));
#159402=CARTESIAN_POINT('Ctrl Pts',(-20.8354165122709,-18.6954967298112,
1.5244124814161));
#159403=CARTESIAN_POINT('Ctrl Pts',(-20.83684279883,-18.7075362599162,1.52367206636053));
#159404=CARTESIAN_POINT('Ctrl Pts',(-20.837371450688,-18.7121273292504,
1.52339064936815));
#159405=CARTESIAN_POINT('Ctrl Pts',(-20.8382824834223,-18.7202738327017,
1.52289298567027));
#159406=CARTESIAN_POINT('Ctrl Pts',(-20.8386708938216,-18.7238285380895,
1.52267640342196));
#159407=CARTESIAN_POINT('Ctrl Pts',(-20.8394063446568,-18.7307210257532,
1.52225757315985));
#159408=CARTESIAN_POINT('Ctrl Pts',(-20.8397544538287,-18.7340586292005,
1.52205526370317));
#159409=CARTESIAN_POINT('Ctrl Pts',(-20.8405037110542,-18.7414117750289,
1.52161063359276));
#159410=CARTESIAN_POINT('Ctrl Pts',(-20.8409013172897,-18.7454276761205,
1.5213685104107));
#159411=CARTESIAN_POINT('Ctrl Pts',(-20.8418560160587,-18.7553599020115,
1.52077138728864));
#159412=CARTESIAN_POINT('Ctrl Pts',(-20.842399689606,-18.7612775228126,
1.5204171133863));
#159413=CARTESIAN_POINT('Ctrl Pts',(-20.8445839011712,-18.786203172463,
1.51893086032492));
#159414=CARTESIAN_POINT('Ctrl Pts',(-20.8459924220239,-18.8052312825265,
1.51781091036615));
#159415=CARTESIAN_POINT('Ctrl Pts',(-20.8496863090444,-18.866345457104,
1.51425344004809));
#159416=CARTESIAN_POINT('Ctrl Pts',(-20.8509723412788,-18.9084830968548,
1.51186063670684));
#159417=CARTESIAN_POINT('Ctrl Pts',(-20.8509995586432,-18.950632994338,
1.50950279134391));
#159418=CARTESIAN_POINT('Ctrl Pts',(-20.7225805737622,-18.2258896078036,
0.755484073133953));
#159419=CARTESIAN_POINT('Ctrl Pts',(-20.7109390354868,-18.1940072148343,
0.757536143489459));
#159420=CARTESIAN_POINT('Ctrl Pts',(-20.6985367298582,-18.1624215432055,
0.759588213844964));
#159421=CARTESIAN_POINT('Ctrl Pts',(-20.6853897265628,-18.1311668043596,
0.761640284200469));
#159422=CARTESIAN_POINT('Ctrl Pts',(-20.6572744224869,-18.0643275051887,
0.766028704948043));
#159423=CARTESIAN_POINT('Ctrl Pts',(-20.6256662206413,-17.9988040174836,
0.770417125695617));
#159424=CARTESIAN_POINT('Ctrl Pts',(-20.5907099139161,-17.9349860888043,
0.774805546443191));
#159425=CARTESIAN_POINT('Ctrl Pts',(-20.555805473251,-17.8712628493194,
0.779187455916675));
#159426=CARTESIAN_POINT('Ctrl Pts',(-20.5175630191303,-17.8092405647745,
0.78356936539016));
#159427=CARTESIAN_POINT('Ctrl Pts',(-20.4761752495541,-17.7492887296441,
0.787951274863645));
#159428=CARTESIAN_POINT('Ctrl Pts',(-20.4348360994882,-17.6894073218137,
0.792328036770722));
#159429=CARTESIAN_POINT('Ctrl Pts',(-20.3903592465927,-17.631591926717,
0.796704798677799));
#159430=CARTESIAN_POINT('Ctrl Pts',(-20.3429822557086,-17.5761856590314,
0.801081560584876));
#159431=CARTESIAN_POINT('Ctrl Pts',(-20.2956353018765,-17.5208145189661,
0.805455547621227));
#159432=CARTESIAN_POINT('Ctrl Pts',(-20.2453921709553,-17.4678498414426,
0.809829534657577));
#159433=CARTESIAN_POINT('Ctrl Pts',(-20.192531655455,-17.4176029164406,
0.814203521693928));
#159434=CARTESIAN_POINT('Ctrl Pts',(-20.1396872205098,-17.3673712769204,
0.818576178131455));
#159435=CARTESIAN_POINT('Ctrl Pts',(-20.084227331126,-17.3198560806449,
0.822948834568982));
#159436=CARTESIAN_POINT('Ctrl Pts',(-20.0264675214797,-17.2753316649021,
0.827321491006509));
#159437=CARTESIAN_POINT('Ctrl Pts',(-19.9687062344823,-17.2308061103364,
0.831694259285623));
#159438=CARTESIAN_POINT('Ctrl Pts',(-19.9086452936504,-17.1892717810647,
0.836067027564738));
#159439=CARTESIAN_POINT('Ctrl Pts',(-19.8466318410332,-17.1509615811096,
0.840439795843852));
#159440=CARTESIAN_POINT('Ctrl Pts',(-19.7845540522246,-17.1126116360308,
0.844817100675033));
#159441=CARTESIAN_POINT('Ctrl Pts',(-19.720520118509,-17.0774927526079,
0.849194405506214));
#159442=CARTESIAN_POINT('Ctrl Pts',(-19.6549038734621,-17.0457930186251,
0.853571710337395));
#159443=CARTESIAN_POINT('Ctrl Pts',(-19.5892518018729,-17.0140759765525,
0.85795140518185));
#159444=CARTESIAN_POINT('Ctrl Pts',(-19.5220161437134,-16.9857819880477,
0.862331100026305));
#159445=CARTESIAN_POINT('Ctrl Pts',(-19.4535904002058,-16.9610508153316,
0.86671079487076));
#159446=CARTESIAN_POINT('Ctrl Pts',(-19.3850434278267,-16.9362758267649,
0.871098249155392));
#159447=CARTESIAN_POINT('Ctrl Pts',(-19.3153026214752,-16.915076399583,
0.875485703440023));
#159448=CARTESIAN_POINT('Ctrl Pts',(-19.2447757398887,-16.897542129042,
0.879873157724655));
#159449=CARTESIAN_POINT('Ctrl Pts',(-19.1968575055399,-16.8856287810247,
0.882854135443738));
#159450=CARTESIAN_POINT('Ctrl Pts',(-19.1485766460487,-16.8754063073494,
0.885835113162821));
#159451=CARTESIAN_POINT('Ctrl Pts',(-19.1000625448657,-16.866889160441,
0.888816090881904));
#159452=CARTESIAN_POINT('Ctrl Pts',(-19.028644802906,-16.8543510450208,
0.8932043963918));
#159453=CARTESIAN_POINT('Ctrl Pts',(-18.9564428168485,-16.8454619385439,
0.897592701901696));
#159454=CARTESIAN_POINT('Ctrl Pts',(-18.8838626572346,-16.8403110588994,
0.901981007411591));
#159455=CARTESIAN_POINT('Ctrl Pts',(-18.8113901761429,-16.8351678210004,
0.906362802516231));
#159456=CARTESIAN_POINT('Ctrl Pts',(-18.7385411124288,-16.8337518342884,
0.910744597620871));
#159457=CARTESIAN_POINT('Ctrl Pts',(-18.6657304379547,-16.8361010735628,
0.915126392725512));
#159458=CARTESIAN_POINT('Ctrl Pts',(-18.5930052675323,-16.8384475540456,
0.919503042139114));
#159459=CARTESIAN_POINT('Ctrl Pts',(-18.5203188765061,-16.8445504614284,
0.923879691552716));
#159460=CARTESIAN_POINT('Ctrl Pts',(-18.4480883417813,-16.854395765714,
0.928256340966318));
#159461=CARTESIAN_POINT('Ctrl Pts',(-18.3759035823937,-16.8642348306421,
0.932630216724654));
#159462=CARTESIAN_POINT('Ctrl Pts',(-18.3041745828625,-16.8778115217113,
0.937004092482989));
#159463=CARTESIAN_POINT('Ctrl Pts',(-18.2333139763946,-16.8950599168264,
0.941377968241324));
#159464=CARTESIAN_POINT('Ctrl Pts',(-18.1624749043755,-16.912303070176,
0.945750514784348));
#159465=CARTESIAN_POINT('Ctrl Pts',(-18.092504169876,-16.9332155982964,
0.950123061327371));
#159466=CARTESIAN_POINT('Ctrl Pts',(-18.0238032220047,-16.9576806834097,
0.954495607870394));
#159467=CARTESIAN_POINT('Ctrl Pts',(-17.9551004924925,-16.9821464029829,
0.958868267807887));
#159468=CARTESIAN_POINT('Ctrl Pts',(-17.8876680687169,-17.0101646987635,
0.96324092774538));
#159469=CARTESIAN_POINT('Ctrl Pts',(-17.8218896690581,-17.0415697489338,
0.967613587682873));
#159470=CARTESIAN_POINT('Ctrl Pts',(-17.7560429779044,-17.0730074039992,
0.971990787339865));
#159471=CARTESIAN_POINT('Ctrl Pts',(-17.6918541756222,-17.1078386254076,
0.976367986996856));
#159472=CARTESIAN_POINT('Ctrl Pts',(-17.6296837442221,-17.1458508900911,
0.980745186653848));
#159473=CARTESIAN_POINT('Ctrl Pts',(-17.5674793440156,-17.183883923993,
0.985124777934071));
#159474=CARTESIAN_POINT('Ctrl Pts',(-17.5072959086028,-17.2251011888991,
0.989504369214295));
#159475=CARTESIAN_POINT('Ctrl Pts',(-17.4494639302801,-17.2692474675138,
0.993883960494518));
#159476=CARTESIAN_POINT('Ctrl Pts',(-17.391529439673,-17.3134719993027,
0.99827131498672));
#159477=CARTESIAN_POINT('Ctrl Pts',(-17.3359550979025,-17.3606356005002,
1.00265866947892));
#159478=CARTESIAN_POINT('Ctrl Pts',(-17.2830369310415,-17.4104439119777,
1.00704602397112));
#159479=CARTESIAN_POINT('Ctrl Pts',(-17.2470699846496,-17.4442971796748,
1.01002798183519));
#159480=CARTESIAN_POINT('Ctrl Pts',(-17.2123293049363,-17.4793713923189,
1.01300993969927));
#159481=CARTESIAN_POINT('Ctrl Pts',(-17.1788971548152,-17.5155654762927,
1.01599189756334));
#159482=CARTESIAN_POINT('Ctrl Pts',(-17.1297001020368,-17.568826850541,
1.02037999518465));
#159483=CARTESIAN_POINT('Ctrl Pts',(-17.083146390969,-17.6247226231684,
1.02476809280597));
#159484=CARTESIAN_POINT('Ctrl Pts',(-17.0395308428605,-17.6829597029633,
1.02915619042728));
#159485=CARTESIAN_POINT('Ctrl Pts',(-16.9959800467907,-17.741110323461,
1.03353777343903));
#159486=CARTESIAN_POINT('Ctrl Pts',(-16.9553590412718,-17.8015949680233,
1.03791935645078));
#159487=CARTESIAN_POINT('Ctrl Pts',(-16.9179243827548,-17.8640853193162,
1.04230093946253));
#159488=CARTESIAN_POINT('Ctrl Pts',(-16.8805337321229,-17.926502207452,
1.04667737152035));
#159489=CARTESIAN_POINT('Ctrl Pts',(-16.8463222340327,-17.9909197065767,
1.05105380357816));
#159490=CARTESIAN_POINT('Ctrl Pts',(-16.8155038596719,-18.0569795759055,
1.05543023563597));
#159491=CARTESIAN_POINT('Ctrl Pts',(-16.7847050391281,-18.1229975311937,
1.05980389091035));
#159492=CARTESIAN_POINT('Ctrl Pts',(-16.7572952741608,-18.1906553530113,
1.06417754618474));
#159493=CARTESIAN_POINT('Ctrl Pts',(-16.7334425000676,-18.259570444403,
1.06855120145912));
#159494=CARTESIAN_POINT('Ctrl Pts',(-16.7095969904912,-18.3284645472576,
1.07292352470848));
#159495=CARTESIAN_POINT('Ctrl Pts',(-16.6893064787907,-18.3986147038968,
1.07729584795784));
#159496=CARTESIAN_POINT('Ctrl Pts',(-16.6726900528573,-18.4696201685282,
1.0816681712072));
#159497=CARTESIAN_POINT('Ctrl Pts',(-16.6560732054628,-18.5406274341515,
1.08604060535674));
#159498=CARTESIAN_POINT('Ctrl Pts',(-16.6431307368287,-18.6124895806671,
1.09041303950627));
#159499=CARTESIAN_POINT('Ctrl Pts',(-16.6339309337084,-18.6847942425672,
1.09478547365581));
#159500=CARTESIAN_POINT('Ctrl Pts',(-16.6247215836389,-18.7571739374787,
1.09916244522925));
#159501=CARTESIAN_POINT('Ctrl Pts',(-16.6192627145554,-18.8299965850532,
1.10353941680269));
#159502=CARTESIAN_POINT('Ctrl Pts',(-16.617570767733,-18.9028440765969,
1.10791638837613));
#159503=CARTESIAN_POINT('Ctrl Pts',(-16.6158778970465,-18.9757313455016,
1.1122957499341));
#159504=CARTESIAN_POINT('Ctrl Pts',(-16.6179560300807,-19.0486430028401,
1.11667511149208));
#159505=CARTESIAN_POINT('Ctrl Pts',(-16.6237694760295,-19.1211630447324,
1.12105447305006));
#159506=CARTESIAN_POINT('Ctrl Pts',(-16.6295932272271,-19.1938116398244,
1.12544159771636));
#159507=CARTESIAN_POINT('Ctrl Pts',(-16.6391654506535,-19.2660667545322,
1.12982872238266));
#159508=CARTESIAN_POINT('Ctrl Pts',(-16.6523988871432,-19.3375201771025,
1.13421584704896));
#159509=CARTESIAN_POINT('Ctrl Pts',(-16.6613997584561,-19.3861200295993,
1.13719979944756));
#159510=CARTESIAN_POINT('Ctrl Pts',(-16.6720933047965,-19.43434921752,1.14018375184616));
#159511=CARTESIAN_POINT('Ctrl Pts',(-16.6844389804884,-19.482083604065,
1.14316770424477));
#159512=CARTESIAN_POINT('Ctrl Pts',(-16.7025947176038,-19.552282513797,
1.14755594970543));
#159513=CARTESIAN_POINT('Ctrl Pts',(-16.7243966050156,-19.6216845828659,
1.1519441951661));
#159514=CARTESIAN_POINT('Ctrl Pts',(-16.7497577488962,-19.6898832488508,
1.15633244062676));
#159515=CARTESIAN_POINT('Ctrl Pts',(-16.7750812549564,-19.757980702952,
1.16071417360537));
#159516=CARTESIAN_POINT('Ctrl Pts',(-16.8039533648488,-19.8248778509223,
1.16509590658397));
#159517=CARTESIAN_POINT('Ctrl Pts',(-16.8362368540352,-19.8901812414549,
1.16947763956257));
#159518=CARTESIAN_POINT('Ctrl Pts',(-16.8684824103679,-19.9554079010014,
1.17385422403833));
#159519=CARTESIAN_POINT('Ctrl Pts',(-16.9041311706798,-20.0190440928805,
1.17823080851409));
#159520=CARTESIAN_POINT('Ctrl Pts',(-16.9429977000799,-20.080715979191,
1.18260739298985));
#159521=CARTESIAN_POINT('Ctrl Pts',(-16.9818395827806,-20.1423487570843,
1.186981202112));
#159522=CARTESIAN_POINT('Ctrl Pts',(-17.0238949293876,-20.2020192938346,
1.19135501123416));
#159523=CARTESIAN_POINT('Ctrl Pts',(-17.0689329083319,-20.2593792794151,
1.19572882035631));
#159524=CARTESIAN_POINT('Ctrl Pts',(-17.1139571835667,-20.316721812068,
1.2001012986592));
#159525=CARTESIAN_POINT('Ctrl Pts',(-17.1619619917057,-20.371754810121,
1.20447377696209));
#159526=CARTESIAN_POINT('Ctrl Pts',(-17.2126748020944,-20.4241612147512,
1.20884625526498));
#159527=CARTESIAN_POINT('Ctrl Pts',(-17.2633889101253,-20.4765689603592,
1.21321884545108));
#159528=CARTESIAN_POINT('Ctrl Pts',(-17.316810821104,-20.5263496338558,
1.21759143563718));
#159529=CARTESIAN_POINT('Ctrl Pts',(-17.3726307376193,-20.5732226039151,
1.22196402582327));
#159530=CARTESIAN_POINT('Ctrl Pts',(-17.4285085838715,-20.6201442185978,
1.22634115386995));
#159531=CARTESIAN_POINT('Ctrl Pts',(-17.4867890342101,-20.6641517941318,
1.23071828191663));
#159532=CARTESIAN_POINT('Ctrl Pts',(-17.5471294002341,-20.7050051852209,
1.23509540996331));
#159533=CARTESIAN_POINT('Ctrl Pts',(-17.607502719815,-20.7458808874863,
1.23947492848171));
#159534=CARTESIAN_POINT('Ctrl Pts',(-17.6699377817392,-20.7835987260512,
1.24385444700011));
#159535=CARTESIAN_POINT('Ctrl Pts',(-17.7340654500449,-20.8179635301383,
1.24823396551851));
#159536=CARTESIAN_POINT('Ctrl Pts',(-17.7983067766523,-20.8523892415588,
1.2526212461878));
#159537=CARTESIAN_POINT('Ctrl Pts',(-17.864246263625,-20.8834498451619,
1.25700852685708));
#159538=CARTESIAN_POINT('Ctrl Pts',(-17.9314934145806,-20.9109977489417,
1.26139580752637));
#159539=CARTESIAN_POINT('Ctrl Pts',(-17.9772094747549,-20.9297254066785,
1.26437837532632));
#159540=CARTESIAN_POINT('Ctrl Pts',(-18.0235294804888,-20.9468306624838,
1.26736094312626));
#159541=CARTESIAN_POINT('Ctrl Pts',(-18.070327288212,-20.9622804609377,
1.27034351092621));
#159542=CARTESIAN_POINT('Ctrl Pts',(-18.1391803753322,-20.9850115752931,
1.27473172931853));
#159543=CARTESIAN_POINT('Ctrl Pts',(-18.2093370332052,-21.0042455878006,
1.27911994771086));
#159544=CARTESIAN_POINT('Ctrl Pts',(-18.2804083784674,-21.0198354965701,
1.28350816610318));
#159545=CARTESIAN_POINT('Ctrl Pts',(-18.3513742469025,-21.0354022683904,
1.28788987195026));
#159546=CARTESIAN_POINT('Ctrl Pts',(-18.4232516406539,-21.0473355700023,
1.29227157779733));
#159547=CARTESIAN_POINT('Ctrl Pts',(-18.4956354572704,-21.0555378163393,
1.2966532836444));
#159548=CARTESIAN_POINT('Ctrl Pts',(-18.5679342235899,-21.0637304251147,
1.30102984102871));
#159549=CARTESIAN_POINT('Ctrl Pts',(-18.6407377537903,-21.068200633326,
1.30540639841303));
#159550=CARTESIAN_POINT('Ctrl Pts',(-18.7136313414975,-21.0689020094824,
1.30978295579735));
#159551=CARTESIAN_POINT('Ctrl Pts',(-18.7864787050571,-21.0696029408739,
1.31415673786712));
#159552=CARTESIAN_POINT('Ctrl Pts',(-18.8594155316466,-21.0665397775258,
1.31853051993688));
#159553=CARTESIAN_POINT('Ctrl Pts',(-18.9320240071873,-21.0597180771103,
1.32290430200665));
#159554=CARTESIAN_POINT('Ctrl Pts',(-19.0046103913194,-21.0528984522235,
1.32727675333636));
#159555=CARTESIAN_POINT('Ctrl Pts',(-19.0768681427674,-21.0423226056621,
1.33164920466608));
#159556=CARTESIAN_POINT('Ctrl Pts',(-19.1483831536915,-21.0280480731276,
1.33602165599579));
#159557=CARTESIAN_POINT('Ctrl Pts',(-19.2198999965103,-21.0137731749434,
1.34039421932815));
#159558=CARTESIAN_POINT('Ctrl Pts',(-19.290673588379,-20.9957994990627,
1.3447667826605));
#159559=CARTESIAN_POINT('Ctrl Pts',(-19.3603002793689,-20.974235634159,
1.34913934599286));
#159560=CARTESIAN_POINT('Ctrl Pts',(-19.4299992351055,-20.9526493883664,
1.35351644755872));
#159561=CARTESIAN_POINT('Ctrl Pts',(-19.4985484515708,-20.9274656569225,
1.35789354912458));
#159562=CARTESIAN_POINT('Ctrl Pts',(-19.5655605178868,-20.8988425989514,
1.36227065069045));
#159563=CARTESIAN_POINT('Ctrl Pts',(-19.6326091841496,-20.870203907939,
1.36665014289569));
#159564=CARTESIAN_POINT('Ctrl Pts',(-19.6981185952225,-20.8381223627168,
1.37102963510093));
#159565=CARTESIAN_POINT('Ctrl Pts',(-19.7617248412387,-20.8028027044234,
1.37540912730617));
#159566=CARTESIAN_POINT('Ctrl Pts',(-19.8254438302969,-20.7674204414965,
1.3797963822282));
#159567=CARTESIAN_POINT('Ctrl Pts',(-19.8872525083671,-20.7287888596301,
1.38418363715023));
#159568=CARTESIAN_POINT('Ctrl Pts',(-19.9468154099209,-20.6871564141191,
1.38857089207226));
#159569=CARTESIAN_POINT('Ctrl Pts',(-19.987311057632,-20.658851331546,1.39155370058405));
#159570=CARTESIAN_POINT('Ctrl Pts',(-20.0267692625344,-20.6291600259051,
1.39453650909585));
#159571=CARTESIAN_POINT('Ctrl Pts',(-20.0650939279425,-20.5981706943675,
1.39751931760764));
#159572=CARTESIAN_POINT('Ctrl Pts',(-20.1207402990933,-20.5531750283627,
1.40185027438838));
#159573=CARTESIAN_POINT('Ctrl Pts',(-20.1742249030448,-20.5052554319719,
1.40618123116912));
#159574=CARTESIAN_POINT('Ctrl Pts',(-20.225218155009,-20.4546501303269,
1.41051218794986));
#159575=CARTESIAN_POINT('Ctrl Pts',(-20.2761246583685,-20.4041309173141,
1.41483577700167));
#159576=CARTESIAN_POINT('Ctrl Pts',(-20.3245478764186,-20.3509354173609,
1.41915936605348));
#159577=CARTESIAN_POINT('Ctrl Pts',(-20.3701907266811,-20.295342438071,
1.42348295510528));
#159578=CARTESIAN_POINT('Ctrl Pts',(-20.4157901278605,-20.2398023797527,
1.427802428376));
#159579=CARTESIAN_POINT('Ctrl Pts',(-20.458614094256,-20.1818697469968,
1.43212190164671));
#159580=CARTESIAN_POINT('Ctrl Pts',(-20.4984028920068,-20.1218595790427,
1.43644137491742));
#159581=CARTESIAN_POINT('Ctrl Pts',(-20.5381677540013,-20.0618855114193,
1.44075824972159));
#159582=CARTESIAN_POINT('Ctrl Pts',(-20.5749007945914,-19.9998367995591,
1.44507512452575));
#159583=CARTESIAN_POINT('Ctrl Pts',(-20.6083841897886,-19.9360594032226,
1.44939199932992));
#159584=CARTESIAN_POINT('Ctrl Pts',(-20.6418591711516,-19.8722980331112,
1.45370778937347));
#159585=CARTESIAN_POINT('Ctrl Pts',(-20.6720858980915,-19.806809280176,
1.45802357941702));
#159586=CARTESIAN_POINT('Ctrl Pts',(-20.6988922427438,-19.7399641326896,
1.46233936946057));
#159587=CARTESIAN_POINT('Ctrl Pts',(-20.7257171905672,-19.6730725957484,
1.46665815459285));
#159588=CARTESIAN_POINT('Ctrl Pts',(-20.7491168267536,-19.6048232442395,
1.47097693972513));
#159589=CARTESIAN_POINT('Ctrl Pts',(-20.7689674510093,-19.5356064370212,
1.4752957248574));
#159590=CARTESIAN_POINT('Ctrl Pts',(-20.788824843842,-19.4663660285662,
1.47961598258968));
#159591=CARTESIAN_POINT('Ctrl Pts',(-20.8051307004056,-19.3961579909125,
1.48393624032195));
#159592=CARTESIAN_POINT('Ctrl Pts',(-20.8178121270028,-19.3253845462204,
1.48825649805423));
#159593=CARTESIAN_POINT('Ctrl Pts',(-20.8305133198985,-19.2545007883054,
1.49258348969011));
#159594=CARTESIAN_POINT('Ctrl Pts',(-20.8395787374245,-19.1830503562126,
1.49691048132598));
#159595=CARTESIAN_POINT('Ctrl Pts',(-20.8449873094553,-19.111441460476,
1.50123747296186));
#159596=CARTESIAN_POINT('Ctrl Pts',(-20.8490314541924,-19.0578974312625,
1.50447288895557));
#159597=CARTESIAN_POINT('Ctrl Pts',(-20.8510321497761,-19.0042649326901,
1.50770830494928));
#159598=CARTESIAN_POINT('Ctrl Pts',(-20.8509996091575,-18.9507135992268,
1.51094372094299));
#159599=CARTESIAN_POINT('Ctrl Pts',(-20.7225805737341,-18.2258896077265,
0.534177427254548));
#159600=CARTESIAN_POINT('Ctrl Pts',(-20.7114372979688,-18.1953717939748,
0.535943861241366));
#159601=CARTESIAN_POINT('Ctrl Pts',(-20.6995928300724,-18.1651141152618,
0.537705172282633));
#159602=CARTESIAN_POINT('Ctrl Pts',(-20.6589739959127,-18.0679971802694,
0.543420718962302));
#159603=CARTESIAN_POINT('Ctrl Pts',(-20.6274486114839,-18.0023487123035,
0.547383506222511));
#159604=CARTESIAN_POINT('Ctrl Pts',(-20.5661675725758,-17.8899733527578,
0.554496467580431));
#159605=CARTESIAN_POINT('Ctrl Pts',(-20.5378433424897,-17.8425464601804,
0.557608819686519));
#159606=CARTESIAN_POINT('Ctrl Pts',(-20.4889702401542,-17.7675400396367,
0.562757567744392));
#159607=CARTESIAN_POINT('Ctrl Pts',(-20.4695464598254,-17.7392575584176,
0.564754091830704));
#159608=CARTESIAN_POINT('Ctrl Pts',(-20.4431385100701,-17.7027400704759,
0.567411422912495));
#159609=CARTESIAN_POINT('Ctrl Pts',(-20.4367658473403,-17.694067855273,
0.568048536260424));
#159610=CARTESIAN_POINT('Ctrl Pts',(-20.4262255985486,-17.6799510508294,
0.569095773986359));
#159611=CARTESIAN_POINT('Ctrl Pts',(-20.4220971448156,-17.6744773843787,
0.569504357168897));
#159612=CARTESIAN_POINT('Ctrl Pts',(-20.41405836778,-17.6639262632964,0.570296901135609));
#159613=CARTESIAN_POINT('Ctrl Pts',(-20.4101514297622,-17.6588463148452,
0.570680724869242));
#159614=CARTESIAN_POINT('Ctrl Pts',(-20.4010835361084,-17.647166032395,
0.571568488047005));
#159615=CARTESIAN_POINT('Ctrl Pts',(-20.3959063681153,-17.640578473631,
0.572073073340858));
#159616=CARTESIAN_POINT('Ctrl Pts',(-20.3818931718824,-17.6229639730359,
0.573432898024445));
#159617=CARTESIAN_POINT('Ctrl Pts',(-20.372985736678,-17.6119946244254,
0.574291013654356));
#159618=CARTESIAN_POINT('Ctrl Pts',(-20.2682887424551,-17.4856678469225,
0.584307120689545));
#159619=CARTESIAN_POINT('Ctrl Pts',(-20.1606326762464,-17.3807345597759,
0.593981586658601));
#159620=CARTESIAN_POINT('Ctrl Pts',(-19.9681082338627,-17.2292981582217,
0.610137882418887));
#159621=CARTESIAN_POINT('Ctrl Pts',(-19.8895209050339,-17.175628199975,
0.616463024077607));
#159622=CARTESIAN_POINT('Ctrl Pts',(-19.7687968862645,-17.1045935663616,
0.625584773392738));
#159623=CARTESIAN_POINT('Ctrl Pts',(-19.7292811432573,-17.0830079998235,
0.628482572713435));
#159624=CARTESIAN_POINT('Ctrl Pts',(-19.6670830654527,-17.0515648159787,
0.63287774179694));
#159625=CARTESIAN_POINT('Ctrl Pts',(-19.6448671952155,-17.0408173890394,
0.63441587117762));
#159626=CARTESIAN_POINT('Ctrl Pts',(-19.6165114206779,-17.0277064543515,
0.636334549577888));
#159627=CARTESIAN_POINT('Ctrl Pts',(-19.6105425854013,-17.0249802398357,
0.636735959007892));
#159628=CARTESIAN_POINT('Ctrl Pts',(-19.6014989849698,-17.0209003661618,
0.637340315751712));
#159629=CARTESIAN_POINT('Ctrl Pts',(-19.5984335811499,-17.0195262307396,
0.637544504456244));
#159630=CARTESIAN_POINT('Ctrl Pts',(-19.5921219984971,-17.0167149464539,
0.637963541107619));
#159631=CARTESIAN_POINT('Ctrl Pts',(-19.5888755231369,-17.0152786873489,
0.638178326549259));
#159632=CARTESIAN_POINT('Ctrl Pts',(-19.581584573337,-17.0120750345173,
0.638659026358099));
#159633=CARTESIAN_POINT('Ctrl Pts',(-19.5775381800954,-17.0103121208095,
0.638924664550785));
#159634=CARTESIAN_POINT('Ctrl Pts',(-19.5672269241606,-17.0058580774846,
0.639598742979764));
#159635=CARTESIAN_POINT('Ctrl Pts',(-19.5609544653994,-17.0031845123946,
0.640006136707957));
#159636=CARTESIAN_POINT('Ctrl Pts',(-19.5252592061529,-16.9881731797153,
0.642310073973924));
#159637=CARTESIAN_POINT('Ctrl Pts',(-19.495571673944,-16.9764707688356,
0.644170640154768));
#159638=CARTESIAN_POINT('Ctrl Pts',(-19.2794561844563,-16.8968775715478,
0.657394736171677));
#159639=CARTESIAN_POINT('Ctrl Pts',(-19.0845520344043,-16.854815391008,
0.667705195132373));
#159640=CARTESIAN_POINT('Ctrl Pts',(-18.8308768713981,-16.8364793507316,
0.681839231662097));
#159641=CARTESIAN_POINT('Ctrl Pts',(-18.7749975640742,-16.8346593857397,
0.684989140635444));
#159642=CARTESIAN_POINT('Ctrl Pts',(-18.6844308353817,-16.8352962157188,
0.690198366812785));
#159643=CARTESIAN_POINT('Ctrl Pts',(-18.6497600394472,-16.8363924185085,
0.692217084492867));
#159644=CARTESIAN_POINT('Ctrl Pts',(-18.6042816533609,-16.838950005534,
0.694903368005656));
#159645=CARTESIAN_POINT('Ctrl Pts',(-18.5934351202104,-16.8396438187457,
0.69554689818027));
#159646=CARTESIAN_POINT('Ctrl Pts',(-18.5756897159066,-16.8409162082112,
0.696604598180517));
#159647=CARTESIAN_POINT('Ctrl Pts',(-18.5687874047928,-16.841445163318,
0.697017208626232));
#159648=CARTESIAN_POINT('Ctrl Pts',(-18.555439136671,-16.8425339820212,
0.697817528158793));
#159649=CARTESIAN_POINT('Ctrl Pts',(-18.5489929004935,-16.8430895622113,
0.69820509847197));
#159650=CARTESIAN_POINT('Ctrl Pts',(-18.5341253637447,-16.8444396381646,
0.699101510073222));
#159651=CARTESIAN_POINT('Ctrl Pts',(-18.5257061175842,-16.8452550689962,
0.699611003538169));
#159652=CARTESIAN_POINT('Ctrl Pts',(-18.5030997550544,-16.847581402876,
0.700984159917421));
#159653=CARTESIAN_POINT('Ctrl Pts',(-18.488922839185,-16.8491852852222,
0.701850727407893));
#159654=CARTESIAN_POINT('Ctrl Pts',(-18.3611876318254,-16.864945667576,
0.709708877508467));
#159655=CARTESIAN_POINT('Ctrl Pts',(-18.2489533345825,-16.8881426257189,
0.716988445908179));
#159656=CARTESIAN_POINT('Ctrl Pts',(-17.9820855705209,-16.9662759357056,
0.735128699931953));
#159657=CARTESIAN_POINT('Ctrl Pts',(-17.8308813018924,-17.0303206101844,
0.746145961979646));
#159658=CARTESIAN_POINT('Ctrl Pts',(-17.6600642190857,-17.1273287319056,
0.758628266601296));
#159659=CARTESIAN_POINT('Ctrl Pts',(-17.6319409962318,-17.1441754721256,
0.760682597349746));
#159660=CARTESIAN_POINT('Ctrl Pts',(-17.5980635973392,-17.1655536783302,
0.763145850395102));
#159661=CARTESIAN_POINT('Ctrl Pts',(-17.5919285120087,-17.1694695820435,
0.763591468481325));
#159662=CARTESIAN_POINT('Ctrl Pts',(-17.5823448931952,-17.175656406651,
0.764286678849229));
#159663=CARTESIAN_POINT('Ctrl Pts',(-17.5788826679878,-17.1779058659089,
0.764537650647354));
#159664=CARTESIAN_POINT('Ctrl Pts',(-17.5724300865637,-17.1821251010458,
0.76500501276939));
#159665=CARTESIAN_POINT('Ctrl Pts',(-17.5694381729535,-17.1840923177264,
0.765221562110266));
#159666=CARTESIAN_POINT('Ctrl Pts',(-17.5626250572158,-17.1885968181109,
0.765714339463772));
#159667=CARTESIAN_POINT('Ctrl Pts',(-17.5588071105342,-17.1911389288376,
0.765990239695704));
#159668=CARTESIAN_POINT('Ctrl Pts',(-17.5471004009189,-17.1989886641076,
0.766835563101407));
#159669=CARTESIAN_POINT('Ctrl Pts',(-17.5392389832897,-17.2043371255787,
0.767402312133544));
#159670=CARTESIAN_POINT('Ctrl Pts',(-17.4690615360394,-17.2527767172425,
0.772455924193651));
#159671=CARTESIAN_POINT('Ctrl Pts',(-17.4090573796301,-17.299136205502,
0.776737454769638));
#159672=CARTESIAN_POINT('Ctrl Pts',(-17.2444599364032,-17.4410420583912,
0.7887679435587));
#159673=CARTESIAN_POINT('Ctrl Pts',(-17.1467956137419,-17.5439843517251,
0.796291846501775));
#159674=CARTESIAN_POINT('Ctrl Pts',(-17.022284352449,-17.7047869375512,
0.807543773762307));
#159675=CARTESIAN_POINT('Ctrl Pts',(-16.9865971547358,-17.7552989850727,
0.811013087338098));
#159676=CARTESIAN_POINT('Ctrl Pts',(-16.9330236195699,-17.8386439593223,
0.81669927307816));
#159677=CARTESIAN_POINT('Ctrl Pts',(-16.913706476478,-17.8705154486512,
0.81886500089717));
#159678=CARTESIAN_POINT('Ctrl Pts',(-16.889721162182,-17.9125536836993,
0.821718118400923));
#159679=CARTESIAN_POINT('Ctrl Pts',(-16.8842775646661,-17.9222718896959,
0.822377440309922));
#159680=CARTESIAN_POINT('Ctrl Pts',(-16.8755513185413,-17.938142947066,
0.823453989790388));
#159681=CARTESIAN_POINT('Ctrl Pts',(-16.8722218878484,-17.9442699345928,
0.823869539519155));
#159682=CARTESIAN_POINT('Ctrl Pts',(-16.8658786503995,-17.9560818189598,
0.824670609821085));
#159683=CARTESIAN_POINT('Ctrl Pts',(-16.8628603670973,-17.9617642336677,
0.825055965522491));
#159684=CARTESIAN_POINT('Ctrl Pts',(-16.8560106148307,-17.9748031584827,
0.825940203282218));
#159685=CARTESIAN_POINT('Ctrl Pts',(-16.8521963996357,-17.9821685690393,
0.826439688171165));
#159686=CARTESIAN_POINT('Ctrl Pts',(-16.8421820600241,-18.0017881881941,
0.82777027896965));
#159687=CARTESIAN_POINT('Ctrl Pts',(-16.8360578054184,-18.014080484588,
0.828604027278096));
#159688=CARTESIAN_POINT('Ctrl Pts',(-16.7905171991408,-18.1077600425731,
0.834959681463982));
#159689=CARTESIAN_POINT('Ctrl Pts',(-16.7562374761297,-18.1915276729902,
0.840658450591947));
#159690=CARTESIAN_POINT('Ctrl Pts',(-16.6828138305152,-18.4098663849784,
0.855532659367458));
#159691=CARTESIAN_POINT('Ctrl Pts',(-16.6514720257712,-18.5466041109191,
0.864884455213787));
#159692=CARTESIAN_POINT('Ctrl Pts',(-16.6269167074976,-18.7400518439375,
0.877655292127132));
#159693=CARTESIAN_POINT('Ctrl Pts',(-16.6221157616113,-18.794940082407,
0.881224237294299));
#159694=CARTESIAN_POINT('Ctrl Pts',(-16.6180913442802,-18.8783338064409,
0.886508468406996));
#159695=CARTESIAN_POINT('Ctrl Pts',(-16.6172932101163,-18.9067374681944,
0.8882839514325));
#159696=CARTESIAN_POINT('Ctrl Pts',(-16.617011841802,-18.9420871916648,
0.890456402204427));
#159697=CARTESIAN_POINT('Ctrl Pts',(-16.6169907237583,-18.9490245832553,
0.890880961869076));
#159698=CARTESIAN_POINT('Ctrl Pts',(-16.6170112734271,-18.9600046128779,
0.891549968285345));
#159699=CARTESIAN_POINT('Ctrl Pts',(-16.6170304186052,-18.9640471716922,
0.891795644361729));
#159700=CARTESIAN_POINT('Ctrl Pts',(-16.6170883622668,-18.9716708854005,
0.892257727471336));
#159701=CARTESIAN_POINT('Ctrl Pts',(-16.6171246676817,-18.9752519529329,
0.892474265406916));
#159702=CARTESIAN_POINT('Ctrl Pts',(-16.6172284551278,-18.9834396489968,
0.892968196498979));
#159703=CARTESIAN_POINT('Ctrl Pts',(-16.617301887279,-18.9880461542013,
0.893245253677383));
#159704=CARTESIAN_POINT('Ctrl Pts',(-16.6175368194362,-19.0002781323422,
0.893978812221056));
#159705=CARTESIAN_POINT('Ctrl Pts',(-16.6177244937206,-19.0079031147136,
0.894433887282302));
#159706=CARTESIAN_POINT('Ctrl Pts',(-16.6193297206289,-19.0613722307344,
0.897610645242317));
#159707=CARTESIAN_POINT('Ctrl Pts',(-16.6221957053312,-19.1071643406512,
0.900257140898366));
#159708=CARTESIAN_POINT('Ctrl Pts',(-16.6301253428469,-19.1903754087313,
0.904988792027944));
#159709=CARTESIAN_POINT('Ctrl Pts',(-16.6347060009862,-19.2278194067312,
0.907089195880349));
#159710=CARTESIAN_POINT('Ctrl Pts',(-16.6596431292772,-19.3945632665945,
0.916389198441517));
#159711=CARTESIAN_POINT('Ctrl Pts',(-16.690963210163,-19.5219305423736,
0.923366387491949));
#159712=CARTESIAN_POINT('Ctrl Pts',(-16.7627867210685,-19.7290523575996,
0.935466793773518));
#159713=CARTESIAN_POINT('Ctrl Pts',(-16.7969202979498,-19.8106104005122,
0.940438829420389));
#159714=CARTESIAN_POINT('Ctrl Pts',(-16.8451368538583,-19.9081936353757,
0.946782341186288));
#159715=CARTESIAN_POINT('Ctrl Pts',(-16.8544956833137,-19.9264607395933,
0.947987351134396));
#159716=CARTESIAN_POINT('Ctrl Pts',(-16.8682707964664,-19.9524109019355,
0.949725690316531));
#159717=CARTESIAN_POINT('Ctrl Pts',(-16.872472196481,-19.9602071546664,
0.950251414748844));
#159718=CARTESIAN_POINT('Ctrl Pts',(-16.8798390522778,-19.9736742905901,
0.951165681465874));
#159719=CARTESIAN_POINT('Ctrl Pts',(-16.882981934529,-19.979357433399,0.951553413430187));
#159720=CARTESIAN_POINT('Ctrl Pts',(-16.8890741879418,-19.9902550926083,
0.952300626729609));
#159721=CARTESIAN_POINT('Ctrl Pts',(-16.8920196450403,-19.9954717342221,
0.952659964537832));
#159722=CARTESIAN_POINT('Ctrl Pts',(-16.8997915754416,-20.0091009990053,
0.953603162015657));
#159723=CARTESIAN_POINT('Ctrl Pts',(-16.904653747497,-20.0174930081285,
0.954188309087466));
#159724=CARTESIAN_POINT('Ctrl Pts',(-16.9217171354945,-20.0464829647469,
0.956225145887692));
#159725=CARTESIAN_POINT('Ctrl Pts',(-16.9342096073345,-20.0669065475066,
0.957687408843258));
#159726=CARTESIAN_POINT('Ctrl Pts',(-17.0303087553724,-20.2181908525007,
0.968729373948781));
#159727=CARTESIAN_POINT('Ctrl Pts',(-17.1277266748375,-20.3396860476931,
0.978845204940532));
#159728=CARTESIAN_POINT('Ctrl Pts',(-17.2901113290746,-20.5019680506941,
0.994012124241926));
#159729=CARTESIAN_POINT('Ctrl Pts',(-17.3454270809017,-20.5517128654059,
0.998935716793171));
#159730=CARTESIAN_POINT('Ctrl Pts',(-17.4390033241238,-20.6273466657035,
1.00677227019052));
#159731=CARTESIAN_POINT('Ctrl Pts',(-17.4756948790863,-20.6550771001664,
1.00973304637029));
#159732=CARTESIAN_POINT('Ctrl Pts',(-17.526918947316,-20.6912307867584,
1.01368767162696));
#159733=CARTESIAN_POINT('Ctrl Pts',(-17.540689410891,-20.7007076005282,
1.01473383051009));
#159734=CARTESIAN_POINT('Ctrl Pts',(-17.5644677100077,-20.7166600941096,
1.01650953185444));
#159735=CARTESIAN_POINT('Ctrl Pts',(-17.5744204528825,-20.7232160551428,
1.01724372037678));
#159736=CARTESIAN_POINT('Ctrl Pts',(-17.5886445411732,-20.732414301111,
1.01827959037356));
#159737=CARTESIAN_POINT('Ctrl Pts',(-17.5928705320101,-20.735125836598,
1.01858568352368));
#159738=CARTESIAN_POINT('Ctrl Pts',(-17.6001691636449,-20.7397723061836,
1.01911141362696));
#159739=CARTESIAN_POINT('Ctrl Pts',(-17.6032371940876,-20.7417144078817,
1.01933152364777));
#159740=CARTESIAN_POINT('Ctrl Pts',(-17.6091970815036,-20.7454656477817,
1.01975737351722));
#159741=CARTESIAN_POINT('Ctrl Pts',(-17.6120883110078,-20.7472756884987,
1.01996317633812));
#159742=CARTESIAN_POINT('Ctrl Pts',(-17.6198979819285,-20.7521386625336,
1.02051700875051));
#159743=CARTESIAN_POINT('Ctrl Pts',(-17.6248246334084,-20.7551784490053,
1.02086417721174));
#159744=CARTESIAN_POINT('Ctrl Pts',(-17.6431403978934,-20.766375964797,
1.02214690229825));
#159745=CARTESIAN_POINT('Ctrl Pts',(-17.6566079166495,-20.7744053183454,
1.02307442104436));
#159746=CARTESIAN_POINT('Ctrl Pts',(-17.7862426501802,-20.8497543212767,
1.03186589672374));
#159747=CARTESIAN_POINT('Ctrl Pts',(-17.9084935466971,-20.9060379904763,
1.03912854476416));
#159748=CARTESIAN_POINT('Ctrl Pts',(-18.186958345739,-21.0034038700418,
1.05514828884175));
#159749=CARTESIAN_POINT('Ctrl Pts',(-18.3441735056854,-21.0389929441575,
1.06389553130149));
#159750=CARTESIAN_POINT('Ctrl Pts',(-18.5224429415701,-21.0584854220862,
1.07436835997818));
#159751=CARTESIAN_POINT('Ctrl Pts',(-18.5410186473761,-21.0602683384654,
1.07546548286871));
#159752=CARTESIAN_POINT('Ctrl Pts',(-18.5681153630046,-21.0625080042181,
1.07707530749207));
#159753=CARTESIAN_POINT('Ctrl Pts',(-18.5766197305491,-21.0631592067393,
1.07758190379785));
#159754=CARTESIAN_POINT('Ctrl Pts',(-18.5915592531959,-21.0642123955715,
1.0784742923869));
#159755=CARTESIAN_POINT('Ctrl Pts',(-18.5979927810334,-21.0646364110575,
1.07885938800254));
#159756=CARTESIAN_POINT('Ctrl Pts',(-18.6105053522581,-21.0654036869368,
1.0796099520909));
#159757=CARTESIAN_POINT('Ctrl Pts',(-18.616584142826,-21.0657501241299,
1.07997531686228));
#159758=CARTESIAN_POINT('Ctrl Pts',(-18.6311459416443,-21.0665170088088,
1.08085233465806));
#159759=CARTESIAN_POINT('Ctrl Pts',(-18.6396301016567,-21.0669126357513,
1.08136476141346));
#159760=CARTESIAN_POINT('Ctrl Pts',(-18.6704145147752,-21.0681625446419,
1.08322946316574));
#159761=CARTESIAN_POINT('Ctrl Pts',(-18.6927249306074,-21.068715223672,
1.08459113297869));
#159762=CARTESIAN_POINT('Ctrl Pts',(-18.8983629553123,-21.0705570774406,
1.09724052907358));
#159763=CARTESIAN_POINT('Ctrl Pts',(-19.0810907955008,-21.0483779831166,
1.10930511710093));
#159764=CARTESIAN_POINT('Ctrl Pts',(-19.3376238586525,-20.9827572732755,
1.12678916331176));
#159765=CARTESIAN_POINT('Ctrl Pts',(-19.4153871112108,-20.9580035463373,
1.13214930867555));
#159766=CARTESIAN_POINT('Ctrl Pts',(-19.5255258326552,-20.9157976128368,
1.13967026937395));
#159767=CARTESIAN_POINT('Ctrl Pts',(-19.5591795901631,-20.9018956947146,
1.14195791219084));
#159768=CARTESIAN_POINT('Ctrl Pts',(-19.5993085682821,-20.8840937375448,
1.14465886514893));
#159769=CARTESIAN_POINT('Ctrl Pts',(-19.6061408200935,-20.8810193163322,
1.14511776581391));
#159770=CARTESIAN_POINT('Ctrl Pts',(-19.6167471219025,-20.8761787542721,
1.14582850047896));
#159771=CARTESIAN_POINT('Ctrl Pts',(-19.6205324434618,-20.87443766791,1.14608182704143));
#159772=CARTESIAN_POINT('Ctrl Pts',(-19.627548579015,-20.8711854152771,
1.14655072293382));
#159773=CARTESIAN_POINT('Ctrl Pts',(-19.6307806854641,-20.8696772730947,
1.14676646819574));
#159774=CARTESIAN_POINT('Ctrl Pts',(-19.63808683347,-20.8662456201758,1.14725358206064));
#159775=CARTESIAN_POINT('Ctrl Pts',(-19.6421585445008,-20.8643172738142,
1.14752464758625));
#159776=CARTESIAN_POINT('Ctrl Pts',(-19.6544481996741,-20.8584488373268,
1.14834167811367));
#159777=CARTESIAN_POINT('Ctrl Pts',(-19.6626470097959,-20.8544686056714,
1.14888521636138));
#159778=CARTESIAN_POINT('Ctrl Pts',(-19.72559356443,-20.8234064000575,1.15304837587856));
#159779=CARTESIAN_POINT('Ctrl Pts',(-19.77917724071,-20.794016751859,1.15653482463366));
#159780=CARTESIAN_POINT('Ctrl Pts',(-19.9708583559331,-20.6778210693829,
1.1690640806586));
#159781=CARTESIAN_POINT('Ctrl Pts',(-20.1000687156637,-20.5774657607867,
1.17766510613336));
#159782=CARTESIAN_POINT('Ctrl Pts',(-20.27310772629,-20.4077224818031,1.19111364917181));
#159783=CARTESIAN_POINT('Ctrl Pts',(-20.3265596928393,-20.349044093169,
1.19560095950127));
#159784=CARTESIAN_POINT('Ctrl Pts',(-20.3888155115893,-20.2724734603528,
1.2013596026769));
#159785=CARTESIAN_POINT('Ctrl Pts',(-20.4008332642335,-20.2572706115,1.20249833136437));
#159786=CARTESIAN_POINT('Ctrl Pts',(-20.417916064501,-20.2350396168923,
1.20415788796861));
#159787=CARTESIAN_POINT('Ctrl Pts',(-20.4231495686117,-20.2281417249908,
1.20467205338954));
#159788=CARTESIAN_POINT('Ctrl Pts',(-20.4322171031043,-20.216036977003,
1.20557309651751));
#159789=CARTESIAN_POINT('Ctrl Pts',(-20.4360698922146,-20.2108442672117,
1.20595923331387));
#159790=CARTESIAN_POINT('Ctrl Pts',(-20.4434805626342,-20.2007601011449,
1.2067083843911));
#159791=CARTESIAN_POINT('Ctrl Pts',(-20.4470413923956,-20.1958708819626,
1.20707127883666));
#159792=CARTESIAN_POINT('Ctrl Pts',(-20.4554655649932,-20.1841992377868,
1.20793685243778));
#159793=CARTESIAN_POINT('Ctrl Pts',(-20.4603098215203,-20.1774032193782,
1.20844026140814));
#159794=CARTESIAN_POINT('Ctrl Pts',(-20.4774343962811,-20.1530760392564,
1.21024031609457));
#159795=CARTESIAN_POINT('Ctrl Pts',(-20.4894885518545,-20.1353879489513,
1.21154553712713));
#159796=CARTESIAN_POINT('Ctrl Pts',(-20.6070116373583,-19.9571883818426,
1.22466380455483));
#159797=CARTESIAN_POINT('Ctrl Pts',(-20.6904215824267,-19.7832402127721,
1.23734172803333));
#159798=CARTESIAN_POINT('Ctrl Pts',(-20.7725200301161,-19.5281126179303,
1.25502394120177));
#159799=CARTESIAN_POINT('Ctrl Pts',(-20.7918958182709,-19.4545296440857,
1.26000957895954));
#159800=CARTESIAN_POINT('Ctrl Pts',(-20.814328049116,-19.3458809039321,
1.26707454839157));
#159801=CARTESIAN_POINT('Ctrl Pts',(-20.8205389602626,-19.3115308797393,
1.26926550463162));
#159802=CARTESIAN_POINT('Ctrl Pts',(-20.8270336493148,-19.2697323491855,
1.2718675311355));
#159803=CARTESIAN_POINT('Ctrl Pts',(-20.8281309522128,-19.2624178821867,
1.27232050370385));
#159804=CARTESIAN_POINT('Ctrl Pts',(-20.8297832007564,-19.2509965662707,
1.2730239599202));
#159805=CARTESIAN_POINT('Ctrl Pts',(-20.8303644475577,-19.246893667125,
1.27327589048324));
#159806=CARTESIAN_POINT('Ctrl Pts',(-20.8314236225284,-19.2392557603439,
1.27374340933906));
#159807=CARTESIAN_POINT('Ctrl Pts',(-20.8319046584578,-19.235721286609,
1.27395916587399));
#159808=CARTESIAN_POINT('Ctrl Pts',(-20.8329764090898,-19.2276946885975,
1.27444781320636));
#159809=CARTESIAN_POINT('Ctrl Pts',(-20.8335616366231,-19.2232018844577,
1.27472039173343));
#159810=CARTESIAN_POINT('Ctrl Pts',(-20.8352591869439,-19.2098348637777,
1.27552867654589));
#159811=CARTESIAN_POINT('Ctrl Pts',(-20.8363297189069,-19.2009553113893,
1.27606208409878));
#159812=CARTESIAN_POINT('Ctrl Pts',(-20.8440773310424,-19.1330752901942,
1.28011463463401));
#159813=CARTESIAN_POINT('Ctrl Pts',(-20.8483264232128,-19.0738184747974,
1.28350787833422));
#159814=CARTESIAN_POINT('Ctrl Pts',(-20.8506770343578,-18.9941772552031,
1.2879671464208));
#159815=CARTESIAN_POINT('Ctrl Pts',(-20.850984040619,-18.9738904697432,
1.28909422412876));
#159816=CARTESIAN_POINT('Ctrl Pts',(-20.8511051846576,-18.8138052346158,
1.29793914602207));
#159817=CARTESIAN_POINT('Ctrl Pts',(-20.8373639019979,-18.6743412751728,
1.30537420899821));
#159818=CARTESIAN_POINT('Ctrl Pts',(-20.7922497677195,-18.4485303721484,
1.31812045243393));
#159819=CARTESIAN_POINT('Ctrl Pts',(-20.7688587895497,-18.3610511026349,
1.32323614162662));
#159820=CARTESIAN_POINT('Ctrl Pts',(-20.7355595833628,-18.2623358416696,
1.32934390222889));
#159821=CARTESIAN_POINT('Ctrl Pts',(-20.7310458567807,-18.2493726096199,
1.33015267371104));
#159822=CARTESIAN_POINT('Ctrl Pts',(-20.7251405052162,-18.232929407642,
1.3311874287854));
#159823=CARTESIAN_POINT('Ctrl Pts',(-20.723865204357,-18.2294077938434,
1.3314095610146));
#159824=CARTESIAN_POINT('Ctrl Pts',(-20.7225805737606,-18.2258896077991,
1.33163200235201));
#159825=CARTESIAN_POINT('Origin',(-18.734,-18.952,0.));
#159826=CARTESIAN_POINT('',(-20.7225805738064,-18.2258896079248,2.35747639166834));
#159827=CARTESIAN_POINT('',(-20.7227693997001,-18.2258206865925,2.13351567424346));
#159828=CARTESIAN_POINT('',(-20.7225805737622,-18.2258896078036,0.));
#159829=CARTESIAN_POINT('Ctrl Pts',(-20.7225805738064,-18.2258896079247,
2.35747639166834));
#159830=CARTESIAN_POINT('Ctrl Pts',(-20.7258083163625,-18.2347293466398,
2.35692313238699));
#159831=CARTESIAN_POINT('Ctrl Pts',(-20.7289770784287,-18.2435905028254,
2.3563679571628));
#159832=CARTESIAN_POINT('Ctrl Pts',(-20.7349196707797,-18.2605645521431,
2.3553032437465));
#159833=CARTESIAN_POINT('Ctrl Pts',(-20.7377034742786,-18.268673656785,
2.35479405363621));
#159834=CARTESIAN_POINT('Ctrl Pts',(-20.742495817349,-18.2829146663808,
2.35389879366171));
#159835=CARTESIAN_POINT('Ctrl Pts',(-20.7445257367668,-18.2890392980362,
2.35351343617493));
#159836=CARTESIAN_POINT('Ctrl Pts',(-20.7484115458976,-18.3009454756058,
2.3527636241521));
#159837=CARTESIAN_POINT('Ctrl Pts',(-20.7502706244422,-18.3067259204055,
2.35239927919822));
#159838=CARTESIAN_POINT('Ctrl Pts',(-20.7546531720662,-18.3205564712627,
2.35152675227654));
#159839=CARTESIAN_POINT('Ctrl Pts',(-20.7571534251839,-18.3286137740462,
2.35101781318275));
#159840=CARTESIAN_POINT('Ctrl Pts',(-20.7659891981977,-18.3577010067049,
2.34917813211045));
#159841=CARTESIAN_POINT('Ctrl Pts',(-20.7720453439938,-18.3788137180527,
2.34783831423605));
#159842=CARTESIAN_POINT('Ctrl Pts',(-20.8265422864376,-18.5805937635665,
2.33498648880404));
#159843=CARTESIAN_POINT('Ctrl Pts',(-20.8511563473918,-18.7668066913728,
2.32266072461913));
#159844=CARTESIAN_POINT('Ctrl Pts',(-20.8509463099784,-19.0167905684345,
2.30615871560825));
#159845=CARTESIAN_POINT('Ctrl Pts',(-20.8480800907388,-19.0797716888197,
2.3020162197331));
#159846=CARTESIAN_POINT('Ctrl Pts',(-20.8379188594366,-19.1922138901616,
2.294736470999));
#159847=CARTESIAN_POINT('Ctrl Pts',(-20.8316744038733,-19.2417244246739,
2.2915721160161));
#159848=CARTESIAN_POINT('Ctrl Pts',(-20.8224344763622,-19.2986864810193,
2.28801336666911));
#159849=CARTESIAN_POINT('Ctrl Pts',(-20.8211403742118,-19.3063940473903,
2.28753358271605));
#159850=CARTESIAN_POINT('Ctrl Pts',(-20.8190058158421,-19.3186899278457,
2.28677117621273));
#159851=CARTESIAN_POINT('Ctrl Pts',(-20.818192841388,-19.3232828519414,
2.2864870599892));
#159852=CARTESIAN_POINT('Ctrl Pts',(-20.8167271896883,-19.3314065696945,
2.28598575937405));
#159853=CARTESIAN_POINT('Ctrl Pts',(-20.8160807013227,-19.3349384359324,
2.28576822723461));
#159854=CARTESIAN_POINT('Ctrl Pts',(-20.8146926433656,-19.3424141738573,
2.28530867660281));
#159855=CARTESIAN_POINT('Ctrl Pts',(-20.8139488464475,-19.346357578959,
2.28506678653678));
#159856=CARTESIAN_POINT('Ctrl Pts',(-20.8119140370227,-19.3569796604932,
2.28441656813197));
#159857=CARTESIAN_POINT('Ctrl Pts',(-20.8106020279226,-19.3636543345662,
2.28400941972416));
#159858=CARTESIAN_POINT('Ctrl Pts',(-20.8039707318822,-19.3965515454561,
2.28200928796493));
#159859=CARTESIAN_POINT('Ctrl Pts',(-20.7981865543776,-19.4226792186793,
2.28044134373731));
#159860=CARTESIAN_POINT('Ctrl Pts',(-20.7800922406585,-19.4976481565181,
2.27598372088627));
#159861=CARTESIAN_POINT('Ctrl Pts',(-20.766532160977,-19.5461709004844,
2.27314943457568));
#159862=CARTESIAN_POINT('Ctrl Pts',(-20.7111897755124,-19.7200192212083,
2.26303191982632));
#159863=CARTESIAN_POINT('Ctrl Pts',(-20.6594361095099,-19.8418489548003,
2.25599598032528));
#159864=CARTESIAN_POINT('Ctrl Pts',(-20.5472452680199,-20.0495631285174,
2.24300928277803));
#159865=CARTESIAN_POINT('Ctrl Pts',(-20.4911569502299,-20.1372841973632,
2.23716716396362));
#159866=CARTESIAN_POINT('Ctrl Pts',(-20.420431863255,-20.2317789747589,
2.2302504123524));
#159867=CARTESIAN_POINT('Ctrl Pts',(-20.4118958807706,-20.2429500581825,
2.22942232056066));
#159868=CARTESIAN_POINT('Ctrl Pts',(-20.3980907442966,-20.2606486717286,
2.22809320824314));
#159869=CARTESIAN_POINT('Ctrl Pts',(-20.3928928723692,-20.2672314572667,
2.22759500934397));
#159870=CARTESIAN_POINT('Ctrl Pts',(-20.3836314092623,-20.278818286173,
2.22671116545395));
#159871=CARTESIAN_POINT('Ctrl Pts',(-20.3795838022371,-20.2838350120582,
2.22632616449098));
#159872=CARTESIAN_POINT('Ctrl Pts',(-20.3711396584803,-20.2942036771062,
2.22552555578883));
#159873=CARTESIAN_POINT('Ctrl Pts',(-20.3667396475099,-20.2995526757355,
2.2251098099924));
#159874=CARTESIAN_POINT('Ctrl Pts',(-20.3553245597693,-20.3132917674634,
2.22403483497759));
#159875=CARTESIAN_POINT('Ctrl Pts',(-20.3482706399931,-20.3216491879681,
2.22337402350214));
#159876=CARTESIAN_POINT('Ctrl Pts',(-20.3180882802634,-20.3568519167258,
2.22056078797073));
#159877=CARTESIAN_POINT('Ctrl Pts',(-20.2943536084299,-20.383167693194,
2.21838335515681));
#159878=CARTESIAN_POINT('Ctrl Pts',(-20.2303135597651,-20.4506846003687,
2.21259364244598));
#159879=CARTESIAN_POINT('Ctrl Pts',(-20.1889687776947,-20.4908550048895,
2.20893880036528));
#159880=CARTESIAN_POINT('Ctrl Pts',(-20.046231988734,-20.618637775003,2.19660006888768));
#159881=CARTESIAN_POINT('Ctrl Pts',(-19.9381730510058,-20.6983093674286,
2.18767365898868));
#159882=CARTESIAN_POINT('Ctrl Pts',(-19.7463729528397,-20.8134091780896,
2.17297285950675));
#159883=CARTESIAN_POINT('Ctrl Pts',(-19.6665527493101,-20.8546540042086,
2.16715233064708));
#159884=CARTESIAN_POINT('Ctrl Pts',(-19.575507996101,-20.8945875652029,
2.16101032812413));
#159885=CARTESIAN_POINT('Ctrl Pts',(-19.5666425072347,-20.8984040226088,
2.160417326593));
#159886=CARTESIAN_POINT('Ctrl Pts',(-19.5535033396687,-20.9039540308319,
2.15954627821453));
#159887=CARTESIAN_POINT('Ctrl Pts',(-19.5492497453426,-20.9057344025882,
2.1592654936668));
#159888=CARTESIAN_POINT('Ctrl Pts',(-19.541688244613,-20.9088703274896,
2.15876852815635));
#159889=CARTESIAN_POINT('Ctrl Pts',(-19.5383826919449,-20.9102314124406,
2.15855201516348));
#159890=CARTESIAN_POINT('Ctrl Pts',(-19.5312874498149,-20.9131319316096,
2.1580888692551));
#159891=CARTESIAN_POINT('Ctrl Pts',(-19.52749675251,-20.9146687533098,2.15784239450916));
#159892=CARTESIAN_POINT('Ctrl Pts',(-19.5170660150691,-20.9188624161717,
2.15716676509725));
#159893=CARTESIAN_POINT('Ctrl Pts',(-19.5104168580256,-20.9214966397538,
2.15673895385215));
#159894=CARTESIAN_POINT('Ctrl Pts',(-19.4746420432678,-20.9354603635601,
2.15445192748817));
#159895=CARTESIAN_POINT('Ctrl Pts',(-19.4452799051509,-20.9461782218498,
2.15262718488174));
#159896=CARTESIAN_POINT('Ctrl Pts',(-19.2606291299342,-21.0089822427048,
2.141412702458));
#159897=CARTESIAN_POINT('Ctrl Pts',(-19.0999558538295,-21.0435551224519,
2.13275781703143));
#159898=CARTESIAN_POINT('Ctrl Pts',(-18.820250477949,-21.070485391847,2.11737630806303));
#159899=CARTESIAN_POINT('Ctrl Pts',(-18.7028972452879,-21.0720110436178,
2.11083594617432));
#159900=CARTESIAN_POINT('Ctrl Pts',(-18.5717696799672,-21.0628232171389,
2.1031352651694));
#159901=CARTESIAN_POINT('Ctrl Pts',(-18.5575209642284,-21.0616797069129,
2.10229349410253));
#159902=CARTESIAN_POINT('Ctrl Pts',(-18.534863540023,-21.0596302271924,
2.10094657192043));
#159903=CARTESIAN_POINT('Ctrl Pts',(-18.5264466385261,-21.0588180043002,
2.10044436437406));
#159904=CARTESIAN_POINT('Ctrl Pts',(-18.5116115644829,-21.0572966720063,
2.0995558624074));
#159905=CARTESIAN_POINT('Ctrl Pts',(-18.5051913109716,-21.0566085801907,
2.09917023444608));
#159906=CARTESIAN_POINT('Ctrl Pts',(-18.4919194259058,-21.0551247165029,
2.09837073803127));
#159907=CARTESIAN_POINT('Ctrl Pts',(-18.4850683423046,-21.05432480972,2.09795674344051));
#159908=CARTESIAN_POINT('Ctrl Pts',(-18.4674940039441,-21.052185785786,
2.09689140910206));
#159909=CARTESIAN_POINT('Ctrl Pts',(-18.4567769694191,-21.0507980287025,
2.09623854082589));
#159910=CARTESIAN_POINT('Ctrl Pts',(-18.4121029180219,-21.0446650132948,
2.09350332907598));
#159911=CARTESIAN_POINT('Ctrl Pts',(-18.3782546353486,-21.0391774262932,
2.0913976723594));
#159912=CARTESIAN_POINT('Ctrl Pts',(-18.2904311488428,-21.0227408786011,
2.08584406996937));
#159913=CARTESIAN_POINT('Ctrl Pts',(-18.2367261495752,-21.01050407104,2.08235775392238));
#159914=CARTESIAN_POINT('Ctrl Pts',(-18.0779620796321,-20.9677537702443,
2.07178969534737));
#159915=CARTESIAN_POINT('Ctrl Pts',(-17.9747308970806,-20.9311806329409,
2.06455955705839));
#159916=CARTESIAN_POINT('Ctrl Pts',(-17.8336087666274,-20.868511289613,
2.05435948503221));
#159917=CARTESIAN_POINT('Ctrl Pts',(-17.7930154194034,-20.8489101446456,
2.05138798456475));
#159918=CARTESIAN_POINT('Ctrl Pts',(-17.7315248675665,-20.8167584669132,
2.04685434478781));
#159919=CARTESIAN_POINT('Ctrl Pts',(-17.7101671044357,-20.8051181280426,
2.04527348681031));
#159920=CARTESIAN_POINT('Ctrl Pts',(-17.6764255488147,-20.785966958465,
2.04277097883368));
#159921=CARTESIAN_POINT('Ctrl Pts',(-17.6639103112282,-20.778692803976,
2.04184164016496));
#159922=CARTESIAN_POINT('Ctrl Pts',(-17.6195514150798,-20.752298002226,
2.03854613601304));
#159923=CARTESIAN_POINT('Ctrl Pts',(-17.5881354689064,-20.7324671883884,
2.03620921284529));
#159924=CARTESIAN_POINT('Ctrl Pts',(-17.5513005739013,-20.7078366624703,
2.0334803912852));
#159925=CARTESIAN_POINT('Ctrl Pts',(-17.5453657376142,-20.7038244522211,
2.0330410817079));
#159926=CARTESIAN_POINT('Ctrl Pts',(-17.5357204643577,-20.6972322411123,
2.03232785449199));
#159927=CARTESIAN_POINT('Ctrl Pts',(-17.5319977767078,-20.694670386801,
2.0320527579364));
#159928=CARTESIAN_POINT('Ctrl Pts',(-17.5253517737041,-20.6900653568766,
2.03156200186602));
#159929=CARTESIAN_POINT('Ctrl Pts',(-17.5224254021448,-20.6880267031779,
2.03134604189937));
#159930=CARTESIAN_POINT('Ctrl Pts',(-17.5161024911806,-20.6835980785477,
2.0308797122341));
#159931=CARTESIAN_POINT('Ctrl Pts',(-17.5127078390562,-20.681205512921,
2.03062952385904));
#159932=CARTESIAN_POINT('Ctrl Pts',(-17.5032535838909,-20.6745003847103,
2.02993316191436));
#159933=CARTESIAN_POINT('Ctrl Pts',(-17.497209565347,-20.6701658070654,
2.02948847196896));
#159934=CARTESIAN_POINT('Ctrl Pts',(-17.4624025899727,-20.6449245143009,
2.02692958108447));
#159935=CARTESIAN_POINT('Ctrl Pts',(-17.4341453339338,-20.6233262899623,
2.02486028058115));
#159936=CARTESIAN_POINT('Ctrl Pts',(-17.3453665331805,-20.5518544541814,
2.01833768880076));
#159937=CARTESIAN_POINT('Ctrl Pts',(-17.2870632426838,-20.4993245016502,
2.01401991869063));
#159938=CARTESIAN_POINT('Ctrl Pts',(-17.0991697150579,-20.3101061416014,
1.99947466152339));
#159939=CARTESIAN_POINT('Ctrl Pts',(-16.9849549549028,-20.1594593255126,
1.98942026280084));
#159940=CARTESIAN_POINT('Ctrl Pts',(-16.8813952245768,-19.9767054546765,
1.97719993950338));
#159941=CARTESIAN_POINT('Ctrl Pts',(-16.8709256924165,-19.9575445265391,
1.9759197804434));
#159942=CARTESIAN_POINT('Ctrl Pts',(-16.8568341383175,-19.9307789084316,
1.97413158216748));
#159943=CARTESIAN_POINT('Ctrl Pts',(-16.8529580873951,-19.923308984707,
1.97363252667585));
#159944=CARTESIAN_POINT('Ctrl Pts',(-16.8463647347101,-19.9104147898239,
1.97277100778911));
#159945=CARTESIAN_POINT('Ctrl Pts',(-16.8436260013233,-19.9050015467289,
1.97240930226415));
#159946=CARTESIAN_POINT('Ctrl Pts',(-16.8380212066333,-19.8938041650189,
1.97166102696565));
#159947=CARTESIAN_POINT('Ctrl Pts',(-16.8351582606411,-19.8880185455322,
1.97127435300053));
#159948=CARTESIAN_POINT('Ctrl Pts',(-16.828546258959,-19.8745014210438,
1.9703708072304));
#159949=CARTESIAN_POINT('Ctrl Pts',(-16.8248177442107,-19.8667600460524,
1.96985322680284));
#159950=CARTESIAN_POINT('Ctrl Pts',(-16.812989494903,-19.8418141593357,
1.96818488786011));
#159951=CARTESIAN_POINT('Ctrl Pts',(-16.8050745787497,-19.8245235131901,
1.96702777548759));
#159952=CARTESIAN_POINT('Ctrl Pts',(-16.7664578113606,-19.7370683256845,
1.96116988338359));
#159953=CARTESIAN_POINT('Ctrl Pts',(-16.7393497961598,-19.6653882738376,
1.95634866999069));
#159954=CARTESIAN_POINT('Ctrl Pts',(-16.6829208435642,-19.4875893693371,
1.94435183652842));
#159955=CARTESIAN_POINT('Ctrl Pts',(-16.6578749468097,-19.3803491484572,
1.93707796735621));
#159956=CARTESIAN_POINT('Ctrl Pts',(-16.6305262316083,-19.2013038494993,
1.92511515039769));
#159957=CARTESIAN_POINT('Ctrl Pts',(-16.6233338488449,-19.1304480869743,
1.92042997292323));
#159958=CARTESIAN_POINT('Ctrl Pts',(-16.61733433675,-19.0122994576882,1.91281694416701));
#159959=CARTESIAN_POINT('Ctrl Pts',(-16.616516366061,-18.9651665585077,
1.90983278489281));
#159960=CARTESIAN_POINT('Ctrl Pts',(-16.6173957729037,-18.9103499265088,
1.90645269333428));
#159961=CARTESIAN_POINT('Ctrl Pts',(-16.6175611038839,-18.9026584768015,
1.90598050484497));
#159962=CARTESIAN_POINT('Ctrl Pts',(-16.6178930520492,-18.890341202341,
1.90522784645326));
#159963=CARTESIAN_POINT('Ctrl Pts',(-16.6180329168794,-18.8857148087221,
1.90494594104846));
#159964=CARTESIAN_POINT('Ctrl Pts',(-16.6183080633057,-18.8775051236416,
1.90444714593629));
#159965=CARTESIAN_POINT('Ctrl Pts',(-16.6184372773653,-18.8739216744508,
1.90422992044497));
#159966=CARTESIAN_POINT('Ctrl Pts',(-16.6187311710324,-18.8663084199623,
1.90376947400334));
#159967=CARTESIAN_POINT('Ctrl Pts',(-16.6188982611728,-18.8622787610035,
1.90352638937618));
#159968=CARTESIAN_POINT('Ctrl Pts',(-16.6193821248796,-18.8513632430997,
1.9028695640882));
#159969=CARTESIAN_POINT('Ctrl Pts',(-16.6197210185941,-18.8444783445676,
1.90245704499849));
#159970=CARTESIAN_POINT('Ctrl Pts',(-16.6215987577909,-18.8097825790151,
1.90038656902143));
#159971=CARTESIAN_POINT('Ctrl Pts',(-16.623652803958,-18.782000929344,1.89875581630666));
#159972=CARTESIAN_POINT('Ctrl Pts',(-16.6312483625306,-18.7010359038296,
1.89406164285005));
#159973=CARTESIAN_POINT('Ctrl Pts',(-16.6382571225494,-18.6480098659028,
1.89106089326304));
#159974=CARTESIAN_POINT('Ctrl Pts',(-16.6709973699999,-18.4564744133057,
1.88031256066668));
#159975=CARTESIAN_POINT('Ctrl Pts',(-16.7085227065561,-18.3203597729883,
1.87282533207767));
#159976=CARTESIAN_POINT('Ctrl Pts',(-16.7922381469642,-18.1037033854721,
1.85997459704055));
#159977=CARTESIAN_POINT('Ctrl Pts',(-16.8306726552981,-18.0206631635639,
1.85480758304878));
#159978=CARTESIAN_POINT('Ctrl Pts',(-16.8809213157937,-17.9282922747449,
1.84864293319504));
#159979=CARTESIAN_POINT('Ctrl Pts',(-16.8876102508442,-17.9162765825241,
1.84783267844201));
#159980=CARTESIAN_POINT('Ctrl Pts',(-16.8985220833874,-17.8971167506601,
1.84652682022565));
#159981=CARTESIAN_POINT('Ctrl Pts',(-16.9026708156669,-17.8899306671746,
1.84603388301395));
#159982=CARTESIAN_POINT('Ctrl Pts',(-16.9101103046585,-17.8772178121379,
1.84515611594288));
#159983=CARTESIAN_POINT('Ctrl Pts',(-16.9133842217187,-17.8716812699107,
1.84477190080306));
#159984=CARTESIAN_POINT('Ctrl Pts',(-16.9202563122077,-17.8601797942408,
1.84396964703329));
#159985=CARTESIAN_POINT('Ctrl Pts',(-16.9238587932814,-17.8542175367383,
1.84355145407345));
#159986=CARTESIAN_POINT('Ctrl Pts',(-16.9332867957635,-17.8387863852644,
1.842463035049));
#159987=CARTESIAN_POINT('Ctrl Pts',(-16.9391575397187,-17.8293454977909,
1.84179115069594));
#159988=CARTESIAN_POINT('Ctrl Pts',(-16.9649382458894,-17.7886060388423,
1.83886542693539));
#159989=CARTESIAN_POINT('Ctrl Pts',(-16.9855935685652,-17.7577890989379,
1.83658402116728));
#159990=CARTESIAN_POINT('Ctrl Pts',(-17.0425763555219,-17.6774222651702,
1.83044611582504));
#159991=CARTESIAN_POINT('Ctrl Pts',(-17.0802671612465,-17.6288866510134,
1.82654041292096));
#159992=CARTESIAN_POINT('Ctrl Pts',(-17.2189499632095,-17.4654980048029,
1.81269808355463));
#159993=CARTESIAN_POINT('Ctrl Pts',(-17.3302137406399,-17.3600065199969,
1.80244490846915));
#159994=CARTESIAN_POINT('Ctrl Pts',(-17.5041023438883,-17.227659279133,
1.78822049381552));
#159995=CARTESIAN_POINT('Ctrl Pts',(-17.5581711048619,-17.1903452798502,
1.78401704030332));
#159996=CARTESIAN_POINT('Ctrl Pts',(-17.6217418817322,-17.1507070044708,
1.77939204599635));
#159997=CARTESIAN_POINT('Ctrl Pts',(-17.6296238945902,-17.1458637918616,
1.77882397340844));
#159998=CARTESIAN_POINT('Ctrl Pts',(-17.64141447723,-17.1387249475169,1.77798247006001));
#159999=CARTESIAN_POINT('Ctrl Pts',(-17.6452989596623,-17.1363900236628,
1.77770655796869));
#160000=CARTESIAN_POINT('Ctrl Pts',(-17.6522544746406,-17.1322394812958,
1.77721492108227));
#160001=CARTESIAN_POINT('Ctrl Pts',(-17.6553226166101,-17.1304191397979,
1.77699889129218));
#160002=CARTESIAN_POINT('Ctrl Pts',(-17.6619642374425,-17.1265013031458,
1.77653306083741));
#160003=CARTESIAN_POINT('Ctrl Pts',(-17.6655392658563,-17.1244065472081,
1.77628343801914));
#160004=CARTESIAN_POINT('Ctrl Pts',(-17.6755107948266,-17.1186030785951,
1.77559024100435));
#160005=CARTESIAN_POINT('Ctrl Pts',(-17.6819206808914,-17.1149173184498,
1.77514812864165));
#160006=CARTESIAN_POINT('Ctrl Pts',(-17.7186588369577,-17.0940477953854,
1.77263327134123));
#160007=CARTESIAN_POINT('Ctrl Pts',(-17.7493904500128,-17.0775805101372,
1.77060363897603));
#160008=CARTESIAN_POINT('Ctrl Pts',(-17.8482673766107,-17.0277014368395,
1.76426104601227));
#160009=CARTESIAN_POINT('Ctrl Pts',(-17.9178121788401,-16.9971888939484,
1.76007512693076));
#160010=CARTESIAN_POINT('Ctrl Pts',(-18.1687670878453,-16.9028176279223,
1.745436893082));
#160011=CARTESIAN_POINT('Ctrl Pts',(-18.3570388578499,-16.8599838383096,
1.73519054994283));
#160012=CARTESIAN_POINT('Ctrl Pts',(-18.5697961078931,-16.8412695656064,
1.72275938408976));
#160013=CARTESIAN_POINT('Ctrl Pts',(-18.5911153024642,-16.8397192897474,
1.72150573952255));
#160014=CARTESIAN_POINT('Ctrl Pts',(-18.6207808065394,-16.8380132490336,
1.71974884791671));
#160015=CARTESIAN_POINT('Ctrl Pts',(-18.6291105179942,-16.8375835881815,
1.71925417367039));
#160016=CARTESIAN_POINT('Ctrl Pts',(-18.6434832158891,-16.8369273585576,
1.718398196058));
#160017=CARTESIAN_POINT('Ctrl Pts',(-18.6495250753707,-16.8366774353009,
1.71803762802359));
#160018=CARTESIAN_POINT('Ctrl Pts',(-18.6620299053607,-16.8362138291616,
1.71728979448245));
#160019=CARTESIAN_POINT('Ctrl Pts',(-18.6684929431349,-16.8360038659546,
1.71690241628587));
#160020=CARTESIAN_POINT('Ctrl Pts',(-18.6836162569328,-16.8355819119939,
1.71599389482369));
#160021=CARTESIAN_POINT('Ctrl Pts',(-18.6922770263912,-16.8353934624515,
1.71547201926492));
#160022=CARTESIAN_POINT('Ctrl Pts',(-18.7203396814472,-16.8349551518393,
1.71377576959262));
#160023=CARTESIAN_POINT('Ctrl Pts',(-18.7397434734032,-16.8349188804873,
1.71259474004215));
#160024=CARTESIAN_POINT('Ctrl Pts',(-18.8386474360854,-16.8360936887253,
1.70653157378616));
#160025=CARTESIAN_POINT('Ctrl Pts',(-18.9180248987222,-16.8415159541797,
1.7015193141454));
#160026=CARTESIAN_POINT('Ctrl Pts',(-19.0942573378354,-16.8635723259758,
1.69007663410652));
#160027=CARTESIAN_POINT('Ctrl Pts',(-19.1906416201142,-16.882509372942,
1.68360009651738));
#160028=CARTESIAN_POINT('Ctrl Pts',(-19.4063500109858,-16.9406972572094,
1.66883648021722));
#160029=CARTESIAN_POINT('Ctrl Pts',(-19.5242191903774,-16.9840177772865,
1.66057003159706));
#160030=CARTESIAN_POINT('Ctrl Pts',(-19.6460713112528,-17.0415280107163,
1.65224947637826));
#160031=CARTESIAN_POINT('Ctrl Pts',(-19.6545425167093,-17.0455953259953,
1.65167233210071));
#160032=CARTESIAN_POINT('Ctrl Pts',(-19.6670850362769,-17.0517205155948,
1.65082006191709));
#160033=CARTESIAN_POINT('Ctrl Pts',(-19.671177101106,-17.0537352961618,
1.65054236272938));
#160034=CARTESIAN_POINT('Ctrl Pts',(-19.6784603842825,-17.05735060567,1.65004878161011));
#160035=CARTESIAN_POINT('Ctrl Pts',(-19.6816540885934,-17.0589459928654,
1.64983258476878));
#160036=CARTESIAN_POINT('Ctrl Pts',(-19.688453827781,-17.0623642636129,
1.64937279273653));
#160037=CARTESIAN_POINT('Ctrl Pts',(-19.692058671699,-17.064189387728,1.64912934088624));
#160038=CARTESIAN_POINT('Ctrl Pts',(-19.7019115533862,-17.0692133698439,
1.64846470424387));
#160039=CARTESIAN_POINT('Ctrl Pts',(-19.7081490069026,-17.0724330324869,
1.64804480499293));
#160040=CARTESIAN_POINT('Ctrl Pts',(-19.7220607645375,-17.0797018900318,
1.64710993832238));
#160041=CARTESIAN_POINT('Ctrl Pts',(-19.7297264643217,-17.0837673857878,
1.64659594184478));
#160042=CARTESIAN_POINT('Ctrl Pts',(-19.7533094442116,-17.0964609814777,
1.64501751795104));
#160043=CARTESIAN_POINT('Ctrl Pts',(-19.7691416062477,-17.1052464452622,
1.64396189282592));
#160044=CARTESIAN_POINT('Ctrl Pts',(-19.8297871908316,-17.1399244212828,
1.63992637847333));
#160045=CARTESIAN_POINT('Ctrl Pts',(-19.8737607067238,-17.1672552772322,
1.63701732715713));
#160046=CARTESIAN_POINT('Ctrl Pts',(-20.0313720688146,-17.273419179665,
1.62649131783225));
#160047=CARTESIAN_POINT('Ctrl Pts',(-20.1382110213948,-17.361716481028,
1.61913727159696));
#160048=CARTESIAN_POINT('Ctrl Pts',(-20.2625557831996,-17.4868515023126,
1.60939918489813));
#160049=CARTESIAN_POINT('Ctrl Pts',(-20.2886957421772,-17.5146190931428,
1.60727671698471));
#160050=CARTESIAN_POINT('Ctrl Pts',(-20.3545778677189,-17.5885041754545,
1.60169997695476));
#160051=CARTESIAN_POINT('Ctrl Pts',(-20.3931038409899,-17.6356539469045,
1.59820821953337));
#160052=CARTESIAN_POINT('Ctrl Pts',(-20.4369346911153,-17.6942818961194,
1.59390846431907));
#160053=CARTESIAN_POINT('Ctrl Pts',(-20.4442396234637,-17.7042332703202,
1.59318007342477));
#160054=CARTESIAN_POINT('Ctrl Pts',(-20.4561120697594,-17.7207070168619,
1.59197634644628));
#160055=CARTESIAN_POINT('Ctrl Pts',(-20.4607306240394,-17.7271923659234,
1.5915029862539));
#160056=CARTESIAN_POINT('Ctrl Pts',(-20.4689812727146,-17.7389173041586,
1.59064805307481));
#160057=CARTESIAN_POINT('Ctrl Pts',(-20.47262650721,-17.7441475625423,1.5902669898041));
#160058=CARTESIAN_POINT('Ctrl Pts',(-20.4803533574746,-17.7553416622544,
1.58945202523937));
#160059=CARTESIAN_POINT('Ctrl Pts',(-20.4844281627048,-17.7613100858529,
1.58901787138294));
#160060=CARTESIAN_POINT('Ctrl Pts',(-20.4953522979815,-17.7774880884497,
1.5878419722303));
#160061=CARTESIAN_POINT('Ctrl Pts',(-20.5021433032203,-17.7877365430192,
1.58709804124387));
#160062=CARTESIAN_POINT('Ctrl Pts',(-20.536092156357,-17.8399516236412,
1.58331219133672));
#160063=CARTESIAN_POINT('Ctrl Pts',(-20.5618449064526,-17.8828086852482,
1.58021863594657));
#160064=CARTESIAN_POINT('Ctrl Pts',(-20.6323246084185,-18.0100994383821,
1.57106281893894));
#160065=CARTESIAN_POINT('Ctrl Pts',(-20.6728801940735,-18.0966912835451,
1.56486873759636));
#160066=CARTESIAN_POINT('Ctrl Pts',(-20.7126288499503,-18.1990579622526,
1.55764706557724));
#160067=CARTESIAN_POINT('Ctrl Pts',(-20.7176731540642,-18.2124497783799,
1.55670439439033));
#160068=CARTESIAN_POINT('Ctrl Pts',(-20.7225805817976,-18.2258896298098,
1.55576077259462));
#160069=CARTESIAN_POINT('',(-20.8479201479212,-18.9528282578495,2.08900081515195));
#160070=CARTESIAN_POINT('Ctrl Pts',(-20.7225805737606,-18.2258896077991,
1.33163200235201));
#160071=CARTESIAN_POINT('Ctrl Pts',(-20.7210219544926,-18.2216210557561,
1.3319018864381));
#160072=CARTESIAN_POINT('Ctrl Pts',(-20.7194496013543,-18.217357549551,
1.33217222556062));
#160073=CARTESIAN_POINT('Ctrl Pts',(-20.7156191687899,-18.2070732799466,
1.33282621705284));
#160074=CARTESIAN_POINT('Ctrl Pts',(-20.7133473748435,-18.2010577141641,
1.33321032421728));
#160075=CARTESIAN_POINT('Ctrl Pts',(-20.7085566090551,-18.1885448558727,
1.33401261267353));
#160076=CARTESIAN_POINT('Ctrl Pts',(-20.7060328960234,-18.1820494725944,
1.33443094956896));
#160077=CARTESIAN_POINT('Ctrl Pts',(-20.6993949332336,-18.1652118167104,
1.33552031141627));
#160078=CARTESIAN_POINT('Ctrl Pts',(-20.695231145335,-18.1548894204065,
1.3361930006093));
#160079=CARTESIAN_POINT('Ctrl Pts',(-20.6767885701682,-18.1101880490247,
1.33912757212948));
#160080=CARTESIAN_POINT('Ctrl Pts',(-20.6616864855575,-18.0761579328253,
1.34141723280241));
#160081=CARTESIAN_POINT('Ctrl Pts',(-20.6191743280709,-17.9867963515471,
1.34758323029482));
#160082=CARTESIAN_POINT('Ctrl Pts',(-20.5902290777744,-17.9322388444417,
1.35150933954297));
#160083=CARTESIAN_POINT('Ctrl Pts',(-20.4847190248718,-17.7527841636449,
1.36495843115519));
#160084=CARTESIAN_POINT('Ctrl Pts',(-20.3975959098247,-17.6345861827553,
1.37476371722997));
#160085=CARTESIAN_POINT('Ctrl Pts',(-20.2858384039415,-17.5119070556623,
1.38559624898239));
#160086=CARTESIAN_POINT('Ctrl Pts',(-20.2724921199729,-17.4976574853576,
1.38686505685932));
#160087=CARTESIAN_POINT('Ctrl Pts',(-20.2223180981013,-17.4455513872136,
1.39153847476712));
#160088=CARTESIAN_POINT('Ctrl Pts',(-20.1842716027264,-17.4088890279648,
1.39489468586293));
#160089=CARTESIAN_POINT('Ctrl Pts',(-20.1384093900395,-17.3678917866915,
1.39868921784772));
#160090=CARTESIAN_POINT('Ctrl Pts',(-20.1318927168922,-17.3621382059105,
1.39922274062836));
#160091=CARTESIAN_POINT('Ctrl Pts',(-20.121966379467,-17.3534824452643,
1.40002664734232));
#160092=CARTESIAN_POINT('Ctrl Pts',(-20.1185827365551,-17.3505507532817,
1.40029915277575));
#160093=CARTESIAN_POINT('Ctrl Pts',(-20.1124893284901,-17.3453049858822,
1.40078711718506));
#160094=CARTESIAN_POINT('Ctrl Pts',(-20.1097830114673,-17.3429870096592,
1.40100286219499));
#160095=CARTESIAN_POINT('Ctrl Pts',(-20.1038860708835,-17.3379620016668,
1.40147083342266));
#160096=CARTESIAN_POINT('Ctrl Pts',(-20.1006932809769,-17.3352576013192,
1.40172286696978));
#160097=CARTESIAN_POINT('Ctrl Pts',(-20.0916937757519,-17.3276804279265,
1.40242958083411));
#160098=CARTESIAN_POINT('Ctrl Pts',(-20.0858688089899,-17.322829294348,
1.40288270525778));
#160099=CARTESIAN_POINT('Ctrl Pts',(-20.0507101727442,-17.2938669780083,
1.40559284898832));
#160100=CARTESIAN_POINT('Ctrl Pts',(-20.0207562176211,-17.2705156445126,
1.40779853364709));
#160101=CARTESIAN_POINT('Ctrl Pts',(-19.9196806853442,-17.1960036163395,
1.41496687867876));
#160102=CARTESIAN_POINT('Ctrl Pts',(-19.8460091755805,-17.1484479461188,
1.41976125592826));
#160103=CARTESIAN_POINT('Ctrl Pts',(-19.6172807610509,-17.020160746121,
1.43402853696588));
#160104=CARTESIAN_POINT('Ctrl Pts',(-19.454997698073,-16.9539150702231,
1.44342150466696));
#160105=CARTESIAN_POINT('Ctrl Pts',(-19.2641706547445,-16.9023318158306,
1.45490744633315));
#160106=CARTESIAN_POINT('Ctrl Pts',(-19.2418171655502,-16.8966795254018,
1.45625815047753));
#160107=CARTESIAN_POINT('Ctrl Pts',(-19.2100738278698,-16.8892023728475,
1.45818538481083));
#160108=CARTESIAN_POINT('Ctrl Pts',(-19.2007565986402,-16.8870741869883,
1.4587521657513));
#160109=CARTESIAN_POINT('Ctrl Pts',(-19.1855972773244,-16.8837194267867,
1.45967623934344));
#160110=CARTESIAN_POINT('Ctrl Pts',(-19.1797637795532,-16.8824543295368,
1.46003229214611));
#160111=CARTESIAN_POINT('Ctrl Pts',(-19.1675440460856,-16.8798583265037,
1.46077912510929));
#160112=CARTESIAN_POINT('Ctrl Pts',(-19.1611568617154,-16.8785322358552,
1.46117005519013));
#160113=CARTESIAN_POINT('Ctrl Pts',(-19.1459515160023,-16.8754485807152,
1.46210209142747));
#160114=CARTESIAN_POINT('Ctrl Pts',(-19.1371281390039,-16.8737176447569,
1.46264404196999));
#160115=CARTESIAN_POINT('Ctrl Pts',(-19.1073845945208,-16.868079208825,
1.46447482370204));
#160116=CARTESIAN_POINT('Ctrl Pts',(-19.0864171273515,-16.8644310704145,
1.46577186589623));
#160117=CARTESIAN_POINT('Ctrl Pts',(-18.9079913323057,-16.8361513397617,
1.47686732111653));
#160118=CARTESIAN_POINT('Ctrl Pts',(-18.7482991778209,-16.829061969009,
1.4872391166112));
#160119=CARTESIAN_POINT('Ctrl Pts',(-18.4580418721694,-16.8489402182039,
1.5064573147894));
#160120=CARTESIAN_POINT('Ctrl Pts',(-18.3278408708816,-16.8701608592363,
1.51519649684384));
#160121=CARTESIAN_POINT('Ctrl Pts',(-18.1852106042422,-16.9073075923962,
1.52439152159694));
#160122=CARTESIAN_POINT('Ctrl Pts',(-18.1700200043961,-16.9114453105206,
1.5253656186187));
#160123=CARTESIAN_POINT('Ctrl Pts',(-18.1492990465425,-16.9173385001607,
1.52668587666152));
#160124=CARTESIAN_POINT('Ctrl Pts',(-18.1437280856433,-16.9189476905789,
1.52703999355517));
#160125=CARTESIAN_POINT('Ctrl Pts',(-18.1348887763288,-16.9215403501383,
1.52760044325141));
#160126=CARTESIAN_POINT('Ctrl Pts',(-18.1316161212942,-16.9225088541452,
1.52780763364718));
#160127=CARTESIAN_POINT('Ctrl Pts',(-18.1248645275822,-16.9245246793535,
1.52823441316738));
#160128=CARTESIAN_POINT('Ctrl Pts',(-18.1213859413173,-16.9255730423128,
1.52845393405084));
#160129=CARTESIAN_POINT('Ctrl Pts',(-18.1131075133796,-16.9280912277091,
1.52897551502527));
#160130=CARTESIAN_POINT('Ctrl Pts',(-18.1083101307743,-16.929569188519,
1.52927710045831));
#160131=CARTESIAN_POINT('Ctrl Pts',(-18.0921660074794,-16.9346057558936,
1.53028986635736));
#160132=CARTESIAN_POINT('Ctrl Pts',(-18.0808437684171,-16.9382429734756,
1.5309965942119));
#160133=CARTESIAN_POINT('Ctrl Pts',(-17.9458033372821,-16.9828828663101,
1.53938988256371));
#160134=CARTESIAN_POINT('Ctrl Pts',(-17.8260773200397,-17.0351373174273,
1.5464801575605));
#160135=CARTESIAN_POINT('Ctrl Pts',(-17.5698310643447,-17.1764098954642,
1.56237647312155));
#160136=CARTESIAN_POINT('Ctrl Pts',(-17.4372483850795,-17.2707987052116,
1.57115794197504));
#160137=CARTESIAN_POINT('Ctrl Pts',(-17.2991238382424,-17.3952783531964,
1.58195474181514));
#160138=CARTESIAN_POINT('Ctrl Pts',(-17.2817684698181,-17.4114561346233,
1.58334401751069));
#160139=CARTESIAN_POINT('Ctrl Pts',(-17.2577289295277,-17.4346318190066,
1.5853169538283));
#160140=CARTESIAN_POINT('Ctrl Pts',(-17.2508148460581,-17.4413894397892,
1.58589021905392));
#160141=CARTESIAN_POINT('Ctrl Pts',(-17.2396930298643,-17.4524095397645,
1.58682197503756));
#160142=CARTESIAN_POINT('Ctrl Pts',(-17.2354566224797,-17.4566429810976,
1.58717918397107));
#160143=CARTESIAN_POINT('Ctrl Pts',(-17.2266556023215,-17.4655127992216,
1.58792611597125));
#160144=CARTESIAN_POINT('Ctrl Pts',(-17.2220942909596,-17.4701523503427,
1.58831597868886));
#160145=CARTESIAN_POINT('Ctrl Pts',(-17.2113461570787,-17.4811861310638,
1.5892412241861));
#160146=CARTESIAN_POINT('Ctrl Pts',(-17.2051781514898,-17.4875984450436,
1.58977741902104));
#160147=CARTESIAN_POINT('Ctrl Pts',(-17.1847724640048,-17.5090818153691,
1.59156897789293));
#160148=CARTESIAN_POINT('Ctrl Pts',(-17.1707161210026,-17.524322756537,
1.59283208234356));
#160149=CARTESIAN_POINT('Ctrl Pts',(-17.0968763169071,-17.6067835057797,
1.59962665289158));
#160150=CARTESIAN_POINT('Ctrl Pts',(-17.0412065289614,-17.6775479476279,
1.60532609872083));
#160151=CARTESIAN_POINT('Ctrl Pts',(-16.9134127850588,-17.8631952220271,
1.61993219425587));
#160152=CARTESIAN_POINT('Ctrl Pts',(-16.8475006227232,-17.9818711046256,
1.62898456836519));
#160153=CARTESIAN_POINT('Ctrl Pts',(-16.7632165096948,-18.1752121343744,
1.64277664843119));
#160154=CARTESIAN_POINT('Ctrl Pts',(-16.7367707097356,-18.2459797246284,
1.64763601727772));
#160155=CARTESIAN_POINT('Ctrl Pts',(-16.7113175913434,-18.3270720321725,
1.65288539227348));
#160156=CARTESIAN_POINT('Ctrl Pts',(-16.7085359778694,-18.3361472627092,
1.65346843799303));
#160157=CARTESIAN_POINT('Ctrl Pts',(-16.7045028214792,-18.3496287054191,
1.65432769977264));
#160158=CARTESIAN_POINT('Ctrl Pts',(-16.7032044327264,-18.3540206199109,
1.65460654983214));
#160159=CARTESIAN_POINT('Ctrl Pts',(-16.7009188439558,-18.3618451308687,
1.65510138478916));
#160160=CARTESIAN_POINT('Ctrl Pts',(-16.6999260703997,-18.3652760391831,
1.65531769101646));
#160161=CARTESIAN_POINT('Ctrl Pts',(-16.6978093832441,-18.3726610066657,
1.65578183770309));
#160162=CARTESIAN_POINT('Ctrl Pts',(-16.6966883049157,-18.3766158199115,
1.65602951240855));
#160163=CARTESIAN_POINT('Ctrl Pts',(-16.6936234206313,-18.387549036666,
1.65671183573583));
#160164=CARTESIAN_POINT('Ctrl Pts',(-16.6917038817193,-18.3945342662098,
1.65714509628754));
#160165=CARTESIAN_POINT('Ctrl Pts',(-16.6813503346419,-18.4329822939229,
1.65951585290567));
#160166=CARTESIAN_POINT('Ctrl Pts',(-16.6736069943411,-18.4646285266987,
1.66141581912851));
#160167=CARTESIAN_POINT('Ctrl Pts',(-16.6315967226036,-18.6552789435078,
1.67262441599101));
#160168=CARTESIAN_POINT('Ctrl Pts',(-16.6150141576487,-18.8176357407558,
1.68122134734676));
#160169=CARTESIAN_POINT('Ctrl Pts',(-16.6187512459146,-19.0971247355112,
1.69652331610837));
#160170=CARTESIAN_POINT('Ctrl Pts',(-16.6299803464647,-19.2135999186024,
1.70304546133171));
#160171=CARTESIAN_POINT('Ctrl Pts',(-16.6532984879152,-19.3426077519539,
1.71072563355701));
#160172=CARTESIAN_POINT('Ctrl Pts',(-16.6559824447445,-19.3566433286477,
1.71156713493904));
#160173=CARTESIAN_POINT('Ctrl Pts',(-16.6604801942807,-19.3789380466631,
1.71291370211074));
#160174=CARTESIAN_POINT('Ctrl Pts',(-16.662201760899,-19.3872155025885,
1.71341582668597));
#160175=CARTESIAN_POINT('Ctrl Pts',(-16.6653254417953,-19.4017957999027,
1.7143042270112));
#160176=CARTESIAN_POINT('Ctrl Pts',(-16.666706902714,-19.4081029904108,
1.7146898367329));
#160177=CARTESIAN_POINT('Ctrl Pts',(-16.6696238845199,-19.4211352011611,
1.715489339632));
#160178=CARTESIAN_POINT('Ctrl Pts',(-16.6711634629842,-19.4278592259625,
1.71590335916317));
#160179=CARTESIAN_POINT('Ctrl Pts',(-16.6751997329196,-19.44509967371,1.71696885089497));
#160180=CARTESIAN_POINT('Ctrl Pts',(-16.6777441292851,-19.4556046220085,
1.71762185256684));
#160181=CARTESIAN_POINT('Ctrl Pts',(-16.6886998391513,-19.4993693525557,
1.72035841401918));
#160182=CARTESIAN_POINT('Ctrl Pts',(-16.6978381780862,-19.5324401560304,
1.72246531639172));
#160183=CARTESIAN_POINT('Ctrl Pts',(-16.7237400580971,-19.618018735276,
1.72802300284975));
#160184=CARTESIAN_POINT('Ctrl Pts',(-16.741756817348,-19.67011717,1.73151222861715));
#160185=CARTESIAN_POINT('Ctrl Pts',(-16.8015463316852,-19.8233666406223,
1.74208586299712));
#160186=CARTESIAN_POINT('Ctrl Pts',(-16.8491460256669,-19.9220407373757,
1.74931865078059));
#160187=CARTESIAN_POINT('Ctrl Pts',(-16.9285119151277,-20.0584575806889,
1.75974409646991));
#160188=CARTESIAN_POINT('Ctrl Pts',(-16.9543026736481,-20.0994812704575,
1.7629376964586));
#160189=CARTESIAN_POINT('Ctrl Pts',(-16.9913860610773,-20.1542052948247,
1.76725022361704));
#160190=CARTESIAN_POINT('Ctrl Pts',(-17.0014762148944,-20.1687013888062,
1.76839776179512));
#160191=CARTESIAN_POINT('Ctrl Pts',(-17.0427697674996,-20.2264706188703,
1.77298712451094));
#160192=CARTESIAN_POINT('Ctrl Pts',(-17.0754251906874,-20.2686873950892,
1.77637848219373));
#160193=CARTESIAN_POINT('Ctrl Pts',(-17.1152358902283,-20.3163195363192,
1.78020794085174));
#160194=CARTESIAN_POINT('Ctrl Pts',(-17.1208694789783,-20.3229759182513,
1.78074315405901));
#160195=CARTESIAN_POINT('Ctrl Pts',(-17.1294614663248,-20.3330015179272,
1.7815491160224));
#160196=CARTESIAN_POINT('Ctrl Pts',(-17.1323896228271,-20.3363963663465,
1.78182200171947));
#160197=CARTESIAN_POINT('Ctrl Pts',(-17.1376648488982,-20.3424732239937,
1.78231038281676));
#160198=CARTESIAN_POINT('Ctrl Pts',(-17.1400079159528,-20.3451586190615,
1.78252616634789));
#160199=CARTESIAN_POINT('Ctrl Pts',(-17.1451137142276,-20.3509806436042,
1.78299391257254));
#160200=CARTESIAN_POINT('Ctrl Pts',(-17.1478789477303,-20.3541150018936,
1.78324568425772));
#160201=CARTESIAN_POINT('Ctrl Pts',(-17.1556718305835,-20.362895582882,
1.78395093748102));
#160202=CARTESIAN_POINT('Ctrl Pts',(-17.1607205268138,-20.3685231587688,
1.78440287335818));
#160203=CARTESIAN_POINT('Ctrl Pts',(-17.1910715248373,-20.4019917354561,
1.78709109148857));
#160204=CARTESIAN_POINT('Ctrl Pts',(-17.2170838484821,-20.4291831623205,
1.78927699878569));
#160205=CARTESIAN_POINT('Ctrl Pts',(-17.305044979401,-20.5163558918042,
1.7963489930711));
#160206=CARTESIAN_POINT('Ctrl Pts',(-17.3699362097486,-20.5732507928181,
1.80107191265039));
#160207=CARTESIAN_POINT('Ctrl Pts',(-17.5777787663376,-20.7341429368544,
1.81537586188073));
#160208=CARTESIAN_POINT('Ctrl Pts',(-17.7303977265982,-20.8243399315862,
1.82486537988993));
#160209=CARTESIAN_POINT('Ctrl Pts',(-17.9134587690612,-20.9036469625251,
1.83645910036613));
#160210=CARTESIAN_POINT('Ctrl Pts',(-17.9346247683343,-20.9124114253736,
1.83780125503696));
#160211=CARTESIAN_POINT('Ctrl Pts',(-17.9647936036023,-20.9243339953728,
1.83971835623945));
#160212=CARTESIAN_POINT('Ctrl Pts',(-17.9736824199401,-20.9277775792068,
1.84028369346282));
#160213=CARTESIAN_POINT('Ctrl Pts',(-17.9881701654244,-20.9332779795624,
1.84120604207386));
#160214=CARTESIAN_POINT('Ctrl Pts',(-17.9937551266535,-20.9353713975967,
1.84156182274692));
#160215=CARTESIAN_POINT('Ctrl Pts',(-18.0054700992802,-20.9397061613955,
1.84230859791443));
#160216=CARTESIAN_POINT('Ctrl Pts',(-18.0116017702445,-20.9419428123586,
1.84269974458839));
#160217=CARTESIAN_POINT('Ctrl Pts',(-18.0262242784434,-20.9472001770425,
1.84363324542762));
#160218=CARTESIAN_POINT('Ctrl Pts',(-18.0347242025274,-20.9501950789746,
1.84417645121177));
#160219=CARTESIAN_POINT('Ctrl Pts',(-18.0634764320616,-20.9601198472911,
1.84601599330436));
#160220=CARTESIAN_POINT('Ctrl Pts',(-18.083814126962,-20.9667966284326,
1.84732064871243));
#160221=CARTESIAN_POINT('Ctrl Pts',(-18.1954346345112,-21.0015751705085,
1.85450219302446));
#160222=CARTESIAN_POINT('Ctrl Pts',(-18.2884261445281,-21.0237795991593,
1.86056924158792));
#160223=CARTESIAN_POINT('Ctrl Pts',(-18.55057327573,-21.0679069297578,1.87784578984168));
#160224=CARTESIAN_POINT('Ctrl Pts',(-18.7213462302002,-21.0758042080899,
1.88933906399189));
#160225=CARTESIAN_POINT('Ctrl Pts',(-18.9278237861098,-21.0604280809679,
1.90255300589767));
#160226=CARTESIAN_POINT('Ctrl Pts',(-18.9643580577657,-21.0567499074251,
1.90486206446987));
#160227=CARTESIAN_POINT('Ctrl Pts',(-19.0078607894498,-21.0512237151479,
1.90756247423834));
#160228=CARTESIAN_POINT('Ctrl Pts',(-19.0149365169512,-21.0502884966069,
1.90800013635016));
#160229=CARTESIAN_POINT('Ctrl Pts',(-19.0264764509981,-21.0487038116536,
1.90871123005467));
#160230=CARTESIAN_POINT('Ctrl Pts',(-19.0309434835953,-21.0480758375145,
1.90898582907012));
#160231=CARTESIAN_POINT('Ctrl Pts',(-19.0389380785928,-21.0469258897975,
1.90947605035841));
#160232=CARTESIAN_POINT('Ctrl Pts',(-19.0424663476806,-21.0464092791225,
1.90969197030715));
#160233=CARTESIAN_POINT('Ctrl Pts',(-19.0501069340053,-21.0452708146114,
1.91015861429498));
#160234=CARTESIAN_POINT('Ctrl Pts',(-19.0542187161271,-21.044645758736,
1.91040915485919));
#160235=CARTESIAN_POINT('Ctrl Pts',(-19.0657052710019,-21.0428649729898,
1.91110749178292));
#160236=CARTESIAN_POINT('Ctrl Pts',(-19.0730758962609,-21.0416823352908,
1.91155379083758));
#160237=CARTESIAN_POINT('Ctrl Pts',(-19.1159589955889,-21.0345687559295,
1.91414068888689));
#160238=CARTESIAN_POINT('Ctrl Pts',(-19.1513240830883,-21.0277712434622,
1.91623523009846));
#160239=CARTESIAN_POINT('Ctrl Pts',(-19.264701771025,-21.0029638676532,
1.92287411602897));
#160240=CARTESIAN_POINT('Ctrl Pts',(-19.3418756446818,-20.9814300577038,
1.92727730868305));
#160241=CARTESIAN_POINT('Ctrl Pts',(-19.5934291658621,-20.8955962683125,
1.94176725306628));
#160242=CARTESIAN_POINT('Ctrl Pts',(-19.7605316247363,-20.8127556969666,
1.95170046577222));
#160243=CARTESIAN_POINT('Ctrl Pts',(-19.9330160070807,-20.6968603277342,
1.96378661426745));
#160244=CARTESIAN_POINT('Ctrl Pts',(-19.9511565896448,-20.6842548111247,
1.96508152927113));
#160245=CARTESIAN_POINT('Ctrl Pts',(-19.9759640131194,-20.6664345708322,
1.96688708733253));
#160246=CARTESIAN_POINT('Ctrl Pts',(-19.9828022141545,-20.6614600124947,
1.96738851347877));
#160247=CARTESIAN_POINT('Ctrl Pts',(-19.9945033272015,-20.6528401734789,
1.96825303460205));
#160248=CARTESIAN_POINT('Ctrl Pts',(-19.9993807174492,-20.6492146512237,
1.96861535943089));
#160249=CARTESIAN_POINT('Ctrl Pts',(-20.0092361051029,-20.6418227250401,
1.96935151421115));
#160250=CARTESIAN_POINT('Ctrl Pts',(-20.0142131874279,-20.6380552064691,
1.9697253856626));
#160251=CARTESIAN_POINT('Ctrl Pts',(-20.0257417283302,-20.6292479326595,
1.97059634111213));
#160252=CARTESIAN_POINT('Ctrl Pts',(-20.0322804456549,-20.6241917359335,
1.97109407196262));
#160253=CARTESIAN_POINT('Ctrl Pts',(-20.0459635004629,-20.6134824016452,
1.97214361526178));
#160254=CARTESIAN_POINT('Ctrl Pts',(-20.0531012773149,-20.6078211901165,
1.972695744184));
#160255=CARTESIAN_POINT('Ctrl Pts',(-20.0720063796626,-20.5926270967978,
1.9741706143622));
#160256=CARTESIAN_POINT('Ctrl Pts',(-20.0837081672744,-20.5830138525671,
1.97509656982422));
#160257=CARTESIAN_POINT('Ctrl Pts',(-20.1190797102583,-20.5533141121942,
1.97793603794961));
#160258=CARTESIAN_POINT('Ctrl Pts',(-20.1424108560363,-20.5328324999823,
1.97986538233887));
#160259=CARTESIAN_POINT('Ctrl Pts',(-20.2894008071012,-20.3979575807575,
1.99239225406707));
#160260=CARTESIAN_POINT('Ctrl Pts',(-20.3994672991205,-20.2696747844113,
2.00357954075189));
#160261=CARTESIAN_POINT('Ctrl Pts',(-20.5482428252334,-20.0474532103545,
2.02119626949266));
#160262=CARTESIAN_POINT('Ctrl Pts',(-20.5974979042015,-19.9613933731637,
2.02764856408787));
#160263=CARTESIAN_POINT('Ctrl Pts',(-20.6447646756313,-19.8634611024349,
2.03436716012927));
#160264=CARTESIAN_POINT('Ctrl Pts',(-20.6489187125123,-19.854701124164,
2.03496283317341));
#160265=CARTESIAN_POINT('Ctrl Pts',(-20.6549630922215,-19.8417253157629,
2.03583703971683));
#160266=CARTESIAN_POINT('Ctrl Pts',(-20.6568999800088,-19.8375314827846,
2.03611833908499));
#160267=CARTESIAN_POINT('Ctrl Pts',(-20.6603117271764,-19.8300802440368,
2.03661587282211));
#160268=CARTESIAN_POINT('Ctrl Pts',(-20.6617920753468,-19.8268254112306,
2.03683244207524));
#160269=CARTESIAN_POINT('Ctrl Pts',(-20.6649460105192,-19.8198439906,2.03729532896275));
#160270=CARTESIAN_POINT('Ctrl Pts',(-20.6666170552115,-19.8161163151537,
2.03754149041177));
#160271=CARTESIAN_POINT('Ctrl Pts',(-20.6711741826595,-19.805871179959,
2.03821537891727));
#160272=CARTESIAN_POINT('Ctrl Pts',(-20.6740381866446,-19.7993438756363,
2.03864177403876));
#160273=CARTESIAN_POINT('Ctrl Pts',(-20.6891489348888,-19.7644269710614,
2.04090765878748));
#160274=CARTESIAN_POINT('Ctrl Pts',(-20.7008062983066,-19.7357845066017,
2.0427134257502));
#160275=CARTESIAN_POINT('Ctrl Pts',(-20.7341848200402,-19.6483324694177,
2.04809763337037));
#160276=CARTESIAN_POINT('Ctrl Pts',(-20.7539265969983,-19.5888013137211,
2.05158937219301));
#160277=CARTESIAN_POINT('Ctrl Pts',(-20.8240164192346,-19.3411372216552,
2.06573528918478));
#160278=CARTESIAN_POINT('Ctrl Pts',(-20.8509329970117,-19.147403052089,
2.07601660755508));
#160279=CARTESIAN_POINT('Ctrl Pts',(-20.8509998750793,-18.9527272648688,
2.08722596880618));
#160280=CARTESIAN_POINT('Ctrl Pts',(-20.7227693997001,-18.2258206865925,
2.13351567424346));
#160281=CARTESIAN_POINT('Ctrl Pts',(-20.8048847893556,-18.4580153825123,
2.11869587583647));
#160282=CARTESIAN_POINT('Ctrl Pts',(-20.8469524796136,-18.7055595108412,
2.10387607742949));
#160283=CARTESIAN_POINT('Ctrl Pts',(-20.8478239065824,-18.9528314138757,
2.0890562790225));
#160284=CARTESIAN_POINT('Origin',(-18.734,-18.952,0.));
#160285=CARTESIAN_POINT('',(-20.7225805742799,-18.2258896092214,3.15472458816501));
#160286=CARTESIAN_POINT('',(-20.7225805736403,-18.2258896074698,2.9354567758078));
#160287=CARTESIAN_POINT('',(-20.7225805737622,-18.2258896078036,0.));
#160288=CARTESIAN_POINT('',(-20.8509999550624,-18.9524361948928,3.11292720174657));
#160289=CARTESIAN_POINT('Ctrl Pts',(-20.7225805742799,-18.2258896092214,
3.15472458816501));
#160290=CARTESIAN_POINT('Ctrl Pts',(-20.7854688877252,-18.398120278352,
3.14471652909388));
#160291=CARTESIAN_POINT('Ctrl Pts',(-20.8257155399036,-18.5777840081126,
3.13493381366904));
#160292=CARTESIAN_POINT('Ctrl Pts',(-20.8447697717378,-18.787446767605,
3.12275006577916));
#160293=CARTESIAN_POINT('Ctrl Pts',(-20.8467072353025,-18.8145415183661,
3.1211630550673));
#160294=CARTESIAN_POINT('Ctrl Pts',(-20.8486554031854,-18.8518703121812,
3.11895650893829));
#160295=CARTESIAN_POINT('Ctrl Pts',(-20.8491140971062,-18.8620790387422,
3.11835100055614));
#160296=CARTESIAN_POINT('Ctrl Pts',(-20.849728275663,-18.8783794155952,
3.11738074779484));
#160297=CARTESIAN_POINT('Ctrl Pts',(-20.8499314061552,-18.8844691911777,
3.11701750020532));
#160298=CARTESIAN_POINT('Ctrl Pts',(-20.8502862993201,-18.8966923163463,
3.11628683852707));
#160299=CARTESIAN_POINT('Ctrl Pts',(-20.8504376956001,-18.9028256166745,
3.11591941655117));
#160300=CARTESIAN_POINT('Ctrl Pts',(-20.8507174561215,-18.9165831187247,
3.11509344704485));
#160301=CARTESIAN_POINT('Ctrl Pts',(-20.8508312920901,-18.924207501338,
3.11463444858109));
#160302=CARTESIAN_POINT('Ctrl Pts',(-20.850969363229,-18.9387001154212,
3.11375954974115));
#160303=CARTESIAN_POINT('Ctrl Pts',(-20.8510013701757,-18.9455681758564,
3.11334390027904));
#160304=CARTESIAN_POINT('Ctrl Pts',(-20.8509999550624,-18.9524361948928,
3.11292720174657));
#160305=CARTESIAN_POINT('Ctrl Pts',(-20.8509999552293,-18.9524353839625,
3.11292725094757));
#160306=CARTESIAN_POINT('Ctrl Pts',(-20.8509977695416,-18.9630630163438,
3.11228244814287));
#160307=CARTESIAN_POINT('Ctrl Pts',(-20.8509155556714,-18.9736903655048,
3.11163514383949));
#160308=CARTESIAN_POINT('Ctrl Pts',(-20.8504244941627,-19.0058552024136,
3.10966822327283));
#160309=CARTESIAN_POINT('Ctrl Pts',(-20.8497669477593,-19.0273869463236,
3.10834094914419));
#160310=CARTESIAN_POINT('Ctrl Pts',(-20.8411521705333,-19.215390635193,
3.09665719184966));
#160311=CARTESIAN_POINT('Ctrl Pts',(-20.8138911677769,-19.3803675993858,
3.08568599821112));
#160312=CARTESIAN_POINT('Ctrl Pts',(-20.7441525987017,-19.6213898137481,
3.06911193324209));
#160313=CARTESIAN_POINT('Ctrl Pts',(-20.7159027153627,-19.7009056435757,
3.06356237554816));
#160314=CARTESIAN_POINT('Ctrl Pts',(-20.6684879343648,-19.812711331155,
3.05581333095038));
#160315=CARTESIAN_POINT('Ctrl Pts',(-20.6530940403106,-19.8465088136624,
3.05347889612171));
#160316=CARTESIAN_POINT('Ctrl Pts',(-20.6335168613556,-19.8866557758572,
3.0507305738603));
#160317=CARTESIAN_POINT('Ctrl Pts',(-20.6301795560165,-19.8934078930938,
3.05026920498877));
#160318=CARTESIAN_POINT('Ctrl Pts',(-20.624937023246,-19.9038737272136,
3.04955558390719));
#160319=CARTESIAN_POINT('Ctrl Pts',(-20.6230567674507,-19.9075997846823,
3.04930181776486));
#160320=CARTESIAN_POINT('Ctrl Pts',(-20.6195502374123,-19.914497796227,
3.04883261078509));
#160321=CARTESIAN_POINT('Ctrl Pts',(-20.6179269857595,-19.9176711749685,
3.04861699097109));
#160322=CARTESIAN_POINT('Ctrl Pts',(-20.6142402441416,-19.9248338996428,
3.04813082924854));
#160323=CARTESIAN_POINT('Ctrl Pts',(-20.6121720748999,-19.9288207767573,
3.04786058619553));
#160324=CARTESIAN_POINT('Ctrl Pts',(-20.6060336744734,-19.9405624023329,
3.04706568169849));
#160325=CARTESIAN_POINT('Ctrl Pts',(-20.6019279348417,-19.948298618839,
3.04654320709552));
#160326=CARTESIAN_POINT('Ctrl Pts',(-20.5720879301076,-20.0036915644863,
3.0428096905925));
#160327=CARTESIAN_POINT('Ctrl Pts',(-20.5445788662825,-20.0503749891729,
3.03970317627656));
#160328=CARTESIAN_POINT('Ctrl Pts',(-20.4249300121516,-20.2366858158767,
3.0272593482136));
#160329=CARTESIAN_POINT('Ctrl Pts',(-20.3181911824819,-20.3662163134544,
3.0184536253374));
#160330=CARTESIAN_POINT('Ctrl Pts',(-20.153980467728,-20.5232860707889,
3.0058658422293));
#160331=CARTESIAN_POINT('Ctrl Pts',(-20.1089106884917,-20.5628706484787,
3.0024966791266));
#160332=CARTESIAN_POINT('Ctrl Pts',(-20.0338325717932,-20.6233628136522,
2.99695987334473));
#160333=CARTESIAN_POINT('Ctrl Pts',(-20.004856256281,-20.6455000770281,
2.99483998983451));
#160334=CARTESIAN_POINT('Ctrl Pts',(-19.9686958267715,-20.6716750179054,
2.99220825633883));
#160335=CARTESIAN_POINT('Ctrl Pts',(-19.9620399704185,-20.6764343362604,
2.99172440933288));
#160336=CARTESIAN_POINT('Ctrl Pts',(-19.9491498834455,-20.6855390121142,
2.99078835132776));
#160337=CARTESIAN_POINT('Ctrl Pts',(-19.9429195097312,-20.6898896289598,
2.99033635047447));
#160338=CARTESIAN_POINT('Ctrl Pts',(-19.9366256366146,-20.694234364416,
2.98988014794073));
#160339=CARTESIAN_POINT('Ctrl Pts',(-19.9365853635496,-20.6942621633299,
2.98987722882094));
#160340=CARTESIAN_POINT('Ctrl Pts',(-19.9365031663644,-20.6943188966083,
2.98987127094159));
#160341=CARTESIAN_POINT('Ctrl Pts',(-19.9364612421273,-20.6943478308812,
2.98986823217493));
#160342=CARTESIAN_POINT('Ctrl Pts',(-19.9363756324267,-20.6944069103868,
2.9898620270206));
#160343=CARTESIAN_POINT('Ctrl Pts',(-19.936331946696,-20.6944370556124,
2.9898588606151));
#160344=CARTESIAN_POINT('Ctrl Pts',(-19.9362426927778,-20.6944986400934,
2.98985239140081));
#160345=CARTESIAN_POINT('Ctrl Pts',(-19.9361971245473,-20.6945300791651,
2.98984908859063));
#160346=CARTESIAN_POINT('Ctrl Pts',(-19.9361039725555,-20.6945943424986,
2.98984233692691));
#160347=CARTESIAN_POINT('Ctrl Pts',(-19.9360563888562,-20.6946271664792,
2.9898388880798));
#160348=CARTESIAN_POINT('Ctrl Pts',(-19.9359590602922,-20.6946942993632,
2.98983183379254));
#160349=CARTESIAN_POINT('Ctrl Pts',(-19.9359093151244,-20.6947286082087,
2.98982822833257));
#160350=CARTESIAN_POINT('Ctrl Pts',(-19.9358075019095,-20.694798821538,
2.98982084910535));
#160351=CARTESIAN_POINT('Ctrl Pts',(-19.9357554337759,-20.6948347257816,
2.98981707533423));
#160352=CARTESIAN_POINT('Ctrl Pts',(-19.9356487962604,-20.6949082519855,
2.98980934656431));
#160353=CARTESIAN_POINT('Ctrl Pts',(-19.9355942266161,-20.6949458737884,
2.9898053915492));
#160354=CARTESIAN_POINT('Ctrl Pts',(-19.9354823876159,-20.6950229709005,
2.98979728591565));
#160355=CARTESIAN_POINT('Ctrl Pts',(-19.9354251180778,-20.6950624459525,
2.98979313528709));
#160356=CARTESIAN_POINT('Ctrl Pts',(-19.9353076583195,-20.6951434007007,
2.98978462242109));
#160357=CARTESIAN_POINT('Ctrl Pts',(-19.9352474679084,-20.6951848800936,
2.98978026017332));
#160358=CARTESIAN_POINT('Ctrl Pts',(-19.9351239193287,-20.6952700124583,
2.98977130617299));
#160359=CARTESIAN_POINT('Ctrl Pts',(-19.9350605609644,-20.6953136650688,
2.98976671441022));
#160360=CARTESIAN_POINT('Ctrl Pts',(-19.9349303993287,-20.6954033332962,
2.98975728130622));
#160361=CARTESIAN_POINT('Ctrl Pts',(-19.9348635957845,-20.6954493485329,
2.98975243994976));
#160362=CARTESIAN_POINT('Ctrl Pts',(-19.9347262313793,-20.695543955459,
2.98974248503145));
#160363=CARTESIAN_POINT('Ctrl Pts',(-19.9346556702405,-20.6955925466861,
2.98973737145472));
#160364=CARTESIAN_POINT('Ctrl Pts',(-19.9345104371643,-20.6956925470043,
2.98972684649496));
#160365=CARTESIAN_POINT('Ctrl Pts',(-19.9344357648919,-20.6957439555701,
2.98972143509373));
#160366=CARTESIAN_POINT('Ctrl Pts',(-19.9342819076382,-20.6958498649359,
2.98971028537758));
#160367=CARTESIAN_POINT('Ctrl Pts',(-19.9342027222522,-20.6959043651356,
2.98970454704035));
#160368=CARTESIAN_POINT('Ctrl Pts',(-19.9340393794748,-20.6960167711766,
2.98969271018984));
#160369=CARTESIAN_POINT('Ctrl Pts',(-19.9339552215973,-20.6960746763246,
2.98968661164954));
#160370=CARTESIAN_POINT('Ctrl Pts',(-19.9337814059067,-20.6961942523361,
2.98967401616129));
#160371=CARTESIAN_POINT('Ctrl Pts',(-19.933691747565,-20.6962559223538,
2.98966751918468));
#160372=CARTESIAN_POINT('Ctrl Pts',(-19.9335063207716,-20.6963834440676,
2.98965408263791));
#160373=CARTESIAN_POINT('Ctrl Pts',(-19.9334105516113,-20.6964492948181,
2.98964714302782));
#160374=CARTESIAN_POINT('Ctrl Pts',(-19.9281812407947,-20.70004432796,2.98926822255984));
#160375=CARTESIAN_POINT('Ctrl Pts',(-19.9230321947558,-20.7035508119744,
2.98889538341952));
#160376=CARTESIAN_POINT('Ctrl Pts',(-19.9113144432798,-20.7114550831538,
2.98804746985103));
#160377=CARTESIAN_POINT('Ctrl Pts',(-19.9047364596769,-20.715838889278,
2.98757187442385));
#160378=CARTESIAN_POINT('Ctrl Pts',(-19.8858604891918,-20.7282664084734,
2.98620816343938));
#160379=CARTESIAN_POINT('Ctrl Pts',(-19.8735032785493,-20.7362189331811,
2.98531665819358));
#160380=CARTESIAN_POINT('Ctrl Pts',(-19.789592024767,-20.7889930289318,
2.97927023993084));
#160381=CARTESIAN_POINT('Ctrl Pts',(-19.7155032841278,-20.8296224716274,
2.97396256013928));
#160382=CARTESIAN_POINT('Ctrl Pts',(-19.5076321377924,-20.9279462165594,
2.95916188623186));
#160383=CARTESIAN_POINT('Ctrl Pts',(-19.3700083212911,-20.9764399912341,
2.94943500180701));
#160384=CARTESIAN_POINT('Ctrl Pts',(-19.1746042461389,-21.0233839295406,
2.93627202266629));
#160385=CARTESIAN_POINT('Ctrl Pts',(-19.1201982756254,-21.0342140189079,
2.93267809635083));
#160386=CARTESIAN_POINT('Ctrl Pts',(-19.0372416454391,-21.0473634162181,
2.92736165187186));
#160387=CARTESIAN_POINT('Ctrl Pts',(-19.0089677533935,-21.0512608847093,
2.92557816504653));
#160388=CARTESIAN_POINT('Ctrl Pts',(-18.9737216628097,-21.0553950642261,
2.92339730987514));
#160389=CARTESIAN_POINT('Ctrl Pts',(-18.9668171222875,-21.0561704927339,
2.92297210937185));
#160390=CARTESIAN_POINT('Ctrl Pts',(-18.9558866591985,-21.0573436000484,
2.92230230791951));
#160391=CARTESIAN_POINT('Ctrl Pts',(-18.9518632705746,-21.057763747376,
2.92205647330538));
#160392=CARTESIAN_POINT('Ctrl Pts',(-18.9442738178413,-21.0585343008492,
2.92159412182861));
#160393=CARTESIAN_POINT('Ctrl Pts',(-18.9407081124935,-21.0588871814911,
2.92137747381635));
#160394=CARTESIAN_POINT('Ctrl Pts',(-18.9325549793725,-21.0596731604716,
2.92088339372251));
#160395=CARTESIAN_POINT('Ctrl Pts',(-18.9279670277192,-21.0601003354403,
2.9206062970677));
#160396=CARTESIAN_POINT('Ctrl Pts',(-18.9157855622333,-21.0611944230948,
2.91987296836841));
#160397=CARTESIAN_POINT('Ctrl Pts',(-18.90818969931,-21.0618353152941,2.91941815837844));
#160398=CARTESIAN_POINT('Ctrl Pts',(-18.855046716413,-21.0660302375047,
2.91625236056243));
#160399=CARTESIAN_POINT('Ctrl Pts',(-18.809394859947,-21.0681503812393,
2.91361588352324));
#160400=CARTESIAN_POINT('Ctrl Pts',(-18.758205340195,-21.0688687659378,
2.91071732448469));
#160401=CARTESIAN_POINT('Ctrl Pts',(-18.7527036805514,-21.0689245248502,
2.91040654571446));
#160402=CARTESIAN_POINT('Ctrl Pts',(-18.7328742176782,-21.0690481857932,
2.90928891640793));
#160403=CARTESIAN_POINT('Ctrl Pts',(-18.7185458293019,-21.0689920809123,
2.90848604356407));
#160404=CARTESIAN_POINT('Ctrl Pts',(-18.6499567126346,-21.0680271008931,
2.90466078417337));
#160405=CARTESIAN_POINT('Ctrl Pts',(-18.5957418468549,-21.0651774867336,
2.90169086503889));
#160406=CARTESIAN_POINT('Ctrl Pts',(-18.4326910601129,-21.050304686801,
2.89277628524882));
#160407=CARTESIAN_POINT('Ctrl Pts',(-18.3246238016806,-21.0319230497364,
2.88688299139122));
#160408=CARTESIAN_POINT('Ctrl Pts',(-18.1648912508766,-20.9918175175315,
2.87772655565901));
#160409=CARTESIAN_POINT('Ctrl Pts',(-18.111866117343,-20.9762749457541,
2.87461210258433));
#160410=CARTESIAN_POINT('Ctrl Pts',(-18.0269372247122,-20.9477284956435,
2.86945763405028));
#160411=CARTESIAN_POINT('Ctrl Pts',(-17.9946353910591,-20.9359883502697,
2.86745721660099));
#160412=CARTESIAN_POINT('Ctrl Pts',(-17.9525628311587,-20.9195268556518,
2.864792789918));
#160413=CARTESIAN_POINT('Ctrl Pts',(-17.9425212660013,-20.9155089466603,
2.86415239441776));
#160414=CARTESIAN_POINT('Ctrl Pts',(-17.9261250296635,-20.9088021456633,
2.86309921054839));
#160415=CARTESIAN_POINT('Ctrl Pts',(-17.919751858174,-20.9061587875014,
2.86268796620739));
#160416=CARTESIAN_POINT('Ctrl Pts',(-17.9074403114557,-20.9009817249937,
2.86188984895989));
#160417=CARTESIAN_POINT('Ctrl Pts',(-17.9015003743258,-20.8984519143574,
2.86150311204705));
#160418=CARTESIAN_POINT('Ctrl Pts',(-17.8878120602564,-20.8925479618631,
2.86060798755312));
#160419=CARTESIAN_POINT('Ctrl Pts',(-17.8800721689093,-20.8891545311906,
2.86009894501476));
#160420=CARTESIAN_POINT('Ctrl Pts',(-17.8593114331308,-20.8799037217195,
2.85872560629793));
#160421=CARTESIAN_POINT('Ctrl Pts',(-17.8463293564329,-20.8739608898477,
2.85785838847722));
#160422=CARTESIAN_POINT('Ctrl Pts',(-17.7276347855214,-20.8181667386345,
2.8498502563495));
#160423=CARTESIAN_POINT('Ctrl Pts',(-17.6261774567779,-20.7597805843482,
2.8424073947021));
#160424=CARTESIAN_POINT('Ctrl Pts',(-17.3962082638498,-20.6007831880577,
2.82414522202982));
#160425=CARTESIAN_POINT('Ctrl Pts',(-17.2734695744201,-20.4931111841494,
2.81318589815666));
#160426=CARTESIAN_POINT('Ctrl Pts',(-17.1424765075164,-20.3483515449723,
2.80078078528216));
#160427=CARTESIAN_POINT('Ctrl Pts',(-17.1212321258497,-20.3237597153163,
2.79874441831563));
#160428=CARTESIAN_POINT('Ctrl Pts',(-17.0959564053863,-20.2931020011724,
2.79630109629527));
#160429=CARTESIAN_POINT('Ctrl Pts',(-17.0913803979649,-20.2874932579013,
2.79585789420545));
#160430=CARTESIAN_POINT('Ctrl Pts',(-17.0842517107691,-20.2786636610299,
2.79516625871425));
#160431=CARTESIAN_POINT('Ctrl Pts',(-17.0816795386985,-20.2754587190938,
2.79491645514562));
#160432=CARTESIAN_POINT('Ctrl Pts',(-17.076889096457,-20.2694540644666,
2.79445078641943));
#160433=CARTESIAN_POINT('Ctrl Pts',(-17.0746686041025,-20.2666562582818,
2.79423476589695));
#160434=CARTESIAN_POINT('Ctrl Pts',(-17.0696159747261,-20.2602567823454,
2.79374281215191));
#160435=CARTESIAN_POINT('Ctrl Pts',(-17.0667884477318,-20.2566515370123,
2.79346720823515));
#160436=CARTESIAN_POINT('Ctrl Pts',(-17.0581333679608,-20.24554176912,2.79262256074521));
#160437=CARTESIAN_POINT('Ctrl Pts',(-17.0523445221673,-20.2380070522076,
2.79205619267762));
#160438=CARTESIAN_POINT('Ctrl Pts',(-16.9739711988061,-20.1345627648873,
2.78436463603442));
#160439=CARTESIAN_POINT('Ctrl Pts',(-16.9096273046158,-20.0326612716488,
2.77776313640976));
#160440=CARTESIAN_POINT('Ctrl Pts',(-16.8042695649171,-19.8292968686495,
2.76529791680799));
#160441=CARTESIAN_POINT('Ctrl Pts',(-16.761768618844,-19.7290532622158,
2.75944056089084));
#160442=CARTESIAN_POINT('Ctrl Pts',(-16.7033687207892,-19.5551650524411,
2.74923475883848));
#160443=CARTESIAN_POINT('Ctrl Pts',(-16.683349675745,-19.4831337259984,
2.74499700951102));
#160444=CARTESIAN_POINT('Ctrl Pts',(-16.6631195411512,-19.391880895208,
2.73953920721983));
#160445=CARTESIAN_POINT('Ctrl Pts',(-16.6593021870224,-19.3735092265777,
2.73843612347462));
#160446=CARTESIAN_POINT('Ctrl Pts',(-16.6541023703782,-19.3466997454833,
2.73681926668054));
#160447=CARTESIAN_POINT('Ctrl Pts',(-16.6525259462666,-19.3383001412871,
2.73631167989067));
#160448=CARTESIAN_POINT('Ctrl Pts',(-16.6498494461607,-19.3235468291119,
2.7354182730538));
#160449=CARTESIAN_POINT('Ctrl Pts',(-16.6487274516848,-19.3171971729287,
2.73503315619491));
#160450=CARTESIAN_POINT('Ctrl Pts',(-16.6466038831833,-19.3048504204276,
2.73428309333823));
#160451=CARTESIAN_POINT('Ctrl Pts',(-16.6455991010574,-19.298853934378,
2.7339182535416));
#160452=CARTESIAN_POINT('Ctrl Pts',(-16.6432569502697,-19.284496897767,
2.73304337763043));
#160453=CARTESIAN_POINT('Ctrl Pts',(-16.641943886623,-19.2761325380828,
2.73253257514694));
#160454=CARTESIAN_POINT('Ctrl Pts',(-16.6373761642577,-19.2458510553143,
2.73067920422813));
#160455=CARTESIAN_POINT('Ctrl Pts',(-16.6344155582316,-19.2238916413541,
2.72932738285842));
#160456=CARTESIAN_POINT('Ctrl Pts',(-16.6099457114204,-19.0180394042224,
2.71657811543212));
#160457=CARTESIAN_POINT('Ctrl Pts',(-16.6123082225007,-18.8321483608013,
2.70438576278502));
#160458=CARTESIAN_POINT('Ctrl Pts',(-16.6503130376275,-18.5693655715215,
2.68685503401444));
#160459=CARTESIAN_POINT('Ctrl Pts',(-16.6663572077965,-18.4904640064932,
2.68156879537342));
#160460=CARTESIAN_POINT('Ctrl Pts',(-16.6960541679284,-18.3777442055429,
2.67413761749523));
#160461=CARTESIAN_POINT('Ctrl Pts',(-16.7061462954959,-18.3430643338559,
2.6718688044231));
#160462=CARTESIAN_POINT('Ctrl Pts',(-16.7193918330655,-18.3015395850717,
2.66918726181472));
#160463=CARTESIAN_POINT('Ctrl Pts',(-16.7216999612358,-18.2944337482181,
2.66872964477093));
#160464=CARTESIAN_POINT('Ctrl Pts',(-16.7253518975084,-18.2833901668765,
2.66802055976474));
#160465=CARTESIAN_POINT('Ctrl Pts',(-16.7266697508931,-18.2794439946736,
2.66776760805705));
#160466=CARTESIAN_POINT('Ctrl Pts',(-16.7291386924514,-18.2721229140524,
2.66729914455568));
#160467=CARTESIAN_POINT('Ctrl Pts',(-16.7302866632742,-18.2687470607406,
2.66708345859834));
#160468=CARTESIAN_POINT('Ctrl Pts',(-16.7329056093276,-18.2611088579796,
2.66659618029708));
#160469=CARTESIAN_POINT('Ctrl Pts',(-16.7343816719604,-18.2568483089747,
2.66632489275421));
#160470=CARTESIAN_POINT('Ctrl Pts',(-16.7388891765665,-18.243970875412,
2.6655063948906));
#160471=CARTESIAN_POINT('Ctrl Pts',(-16.7419628328504,-18.2353687346147,
2.66496162505084));
#160472=CARTESIAN_POINT('Ctrl Pts',(-16.7662514808348,-18.1687567801591,
2.66075661548381));
#160473=CARTESIAN_POINT('Ctrl Pts',(-16.7899425478092,-18.111674877791,
2.65723262273757));
#160474=CARTESIAN_POINT('Ctrl Pts',(-16.8367902575373,-18.0114295815509,
2.65105075814918));
#160475=CARTESIAN_POINT('Ctrl Pts',(-16.859009674805,-17.9678815348047,
2.64836766705726));
#160476=CARTESIAN_POINT('Ctrl Pts',(-16.8870843797334,-17.9172668203226,
2.64521014660781));
#160477=CARTESIAN_POINT('Ctrl Pts',(-16.8915017216318,-17.9094213906173,
2.64471959100856));
#160478=CARTESIAN_POINT('Ctrl Pts',(-16.9501145785086,-17.8068578955759,
2.63828892504994));
#160479=CARTESIAN_POINT('Ctrl Pts',(-17.0115045676925,-17.7164409311076,
2.63241175022768));
#160480=CARTESIAN_POINT('Ctrl Pts',(-17.1265997777106,-17.5722786641264,
2.62215224693034));
#160481=CARTESIAN_POINT('Ctrl Pts',(-17.1767171591789,-17.515951647562,
2.61788011849854));
#160482=CARTESIAN_POINT('Ctrl Pts',(-17.2429895847003,-17.4490255357458,
2.61238088307276));
#160483=CARTESIAN_POINT('Ctrl Pts',(-17.2564304908981,-17.4358098369583,
2.61127283436402));
#160484=CARTESIAN_POINT('Ctrl Pts',(-17.2762305823069,-17.4168548494912,
2.60965002467063));
#160485=CARTESIAN_POINT('Ctrl Pts',(-17.2824511916493,-17.4109716543871,
2.60914151530343));
#160486=CARTESIAN_POINT('Ctrl Pts',(-17.2934205574522,-17.4007226301013,
2.60824704262147));
#160487=CARTESIAN_POINT('Ctrl Pts',(-17.2981539270113,-17.3963404415128,
2.60786178778093));
#160488=CARTESIAN_POINT('Ctrl Pts',(-17.3073842221779,-17.3878729803363,
2.6071118711392));
#160489=CARTESIAN_POINT('Ctrl Pts',(-17.3118788560945,-17.3837852946636,
2.60674731748892));
#160490=CARTESIAN_POINT('Ctrl Pts',(-17.3226661612164,-17.3740591948397,
2.60587379902979));
#160491=CARTESIAN_POINT('Ctrl Pts',(-17.328975077989,-17.368439027263,2.60536407319583));
#160492=CARTESIAN_POINT('Ctrl Pts',(-17.3518656256528,-17.3482919369598,
2.6035186372327));
#160493=CARTESIAN_POINT('Ctrl Pts',(-17.3686398296293,-17.3339868579936,
2.60217377705548));
#160494=CARTESIAN_POINT('Ctrl Pts',(-17.5292275944535,-17.2013128164937,
2.58936426040597));
#160495=CARTESIAN_POINT('Ctrl Pts',(-17.6878248408545,-17.1021697917924,
2.57709367830812));
#160496=CARTESIAN_POINT('Ctrl Pts',(-17.9298504657469,-16.9920544581515,
2.55953971340276));
#160497=CARTESIAN_POINT('Ctrl Pts',(-18.0042174964672,-16.9631656175317,
2.55430347000594));
#160498=CARTESIAN_POINT('Ctrl Pts',(-18.1141968763846,-16.9274450428546,
2.54693294721454));
#160499=CARTESIAN_POINT('Ctrl Pts',(-18.1486318589578,-16.9172215892222,
2.54467686267104));
#160500=CARTESIAN_POINT('Ctrl Pts',(-18.1905148927086,-16.9059382763945,
2.54200829632643));
#160501=CARTESIAN_POINT('Ctrl Pts',(-18.1977275695632,-16.9040360054894,
2.54155142231712));
#160502=CARTESIAN_POINT('Ctrl Pts',(-18.2089760932919,-16.9011328214072,
2.54084323595441));
#160503=CARTESIAN_POINT('Ctrl Pts',(-18.2130050065336,-16.9001056303226,
2.54059044580314));
#160504=CARTESIAN_POINT('Ctrl Pts',(-18.2204950067648,-16.8982195009416,
2.54012212885059));
#160505=CARTESIAN_POINT('Ctrl Pts',(-18.223955204804,-16.8973574462796,
2.53990642884282));
#160506=CARTESIAN_POINT('Ctrl Pts',(-18.2317990320718,-16.8954243144646,
2.5394189248014));
#160507=CARTESIAN_POINT('Ctrl Pts',(-18.2361839063009,-16.8943585102735,
2.53914742676615));
#160508=CARTESIAN_POINT('Ctrl Pts',(-18.2475178980138,-16.8916419780715,
2.53844823370985));
#160509=CARTESIAN_POINT('Ctrl Pts',(-18.2544720864198,-16.8900123672903,
2.53802172425676));
#160510=CARTESIAN_POINT('Ctrl Pts',(-18.2973029754371,-16.8802039855284,
2.53540942859809));
#160511=CARTESIAN_POINT('Ctrl Pts',(-18.3333819803645,-16.8729260266833,
2.53327173696836));
#160512=CARTESIAN_POINT('Ctrl Pts',(-18.5372414799472,-16.8373074260169,
2.5214516820225));
#160513=CARTESIAN_POINT('Ctrl Pts',(-18.7077820129277,-16.8283326084829,
2.5124979413225));
#160514=CARTESIAN_POINT('Ctrl Pts',(-18.972930236559,-16.8463559883984,
2.49788030651757));
#160515=CARTESIAN_POINT('Ctrl Pts',(-19.0677304202319,-16.8592875780321,
2.4925218126008));
#160516=CARTESIAN_POINT('Ctrl Pts',(-19.1822990539436,-16.8828998331049,
2.48571043485678));
#160517=CARTESIAN_POINT('Ctrl Pts',(-19.2032044840941,-16.8875401081621,
2.48445396354954));
#160518=CARTESIAN_POINT('Ctrl Pts',(-19.2328041060998,-16.8945830010857,
2.48265418015873));
#160519=CARTESIAN_POINT('Ctrl Pts',(-19.2415593115042,-16.8967253747583,
2.48211922995132));
#160520=CARTESIAN_POINT('Ctrl Pts',(-19.2566304773285,-16.9005154187311,
2.48119378142771));
#160521=CARTESIAN_POINT('Ctrl Pts',(-19.262953036607,-16.9021365200069,
2.48080414563087));
#160522=CARTESIAN_POINT('Ctrl Pts',(-19.2750382247347,-16.9052947917458,
2.4800566633041));
#160523=CARTESIAN_POINT('Ctrl Pts',(-19.2808020609307,-16.9068271282971,
2.47969897674571));
#160524=CARTESIAN_POINT('Ctrl Pts',(-19.295759695732,-16.9108714200591,
2.47876762629992));
#160525=CARTESIAN_POINT('Ctrl Pts',(-19.3049430676765,-16.9134211213627,
2.47819274066827));
#160526=CARTESIAN_POINT('Ctrl Pts',(-19.336129882992,-16.9223071903796,
2.47622976998112));
#160527=CARTESIAN_POINT('Ctrl Pts',(-19.3580470117735,-16.9289383202925,
2.47483212517879));
#160528=CARTESIAN_POINT('Ctrl Pts',(-19.5481992773025,-16.989853739395,
2.46254314141727));
#160529=CARTESIAN_POINT('Ctrl Pts',(-19.709098980589,-17.0646482972645,
2.4509363949218));
#160530=CARTESIAN_POINT('Ctrl Pts',(-19.9317544890571,-17.2042903791135,
2.43357259671966));
#160531=CARTESIAN_POINT('Ctrl Pts',(-20.001853531418,-17.2544564655524,
2.4278993392237));
#160532=CARTESIAN_POINT('Ctrl Pts',(-20.0978870801496,-17.3324585809217,
2.42000187112837));
#160533=CARTESIAN_POINT('Ctrl Pts',(-20.1264343243009,-17.3569359162561,
2.41763741074223));
#160534=CARTESIAN_POINT('Ctrl Pts',(-20.1599214149946,-17.3872334833199,
2.41485859842912));
#160535=CARTESIAN_POINT('Ctrl Pts',(-20.165499358589,-17.3923347398302,
2.41439555569302));
#160536=CARTESIAN_POINT('Ctrl Pts',(-20.1741189386858,-17.400302893632,
2.41367991162881));
#160537=CARTESIAN_POINT('Ctrl Pts',(-20.1771795439561,-17.4031490478177,
2.41342578281701));
#160538=CARTESIAN_POINT('Ctrl Pts',(-20.1828344133771,-17.4084390052608,
2.41295624221562));
#160539=CARTESIAN_POINT('Ctrl Pts',(-20.1854309123638,-17.410880274347,
2.41274064931245));
#160540=CARTESIAN_POINT('Ctrl Pts',(-20.1912800749276,-17.4164076432322,
2.41225497327949));
#160541=CARTESIAN_POINT('Ctrl Pts',(-20.194529097568,-17.4194975174728,
2.41198518640582));
#160542=CARTESIAN_POINT('Ctrl Pts',(-20.2040695561237,-17.4286285493413,
2.41119286584023));
#160543=CARTESIAN_POINT('Ctrl Pts',(-20.210333590182,-17.4346983777288,
2.41067249781152));
#160544=CARTESIAN_POINT('Ctrl Pts',(-20.254664251811,-17.4781890914558,
2.40698720276468));
#160545=CARTESIAN_POINT('Ctrl Pts',(-20.2913444518108,-17.5170025642334,
2.40392378474618));
#160546=CARTESIAN_POINT('Ctrl Pts',(-20.3355342809387,-17.5674552793871,
2.40015208423915));
#160547=CARTESIAN_POINT('Ctrl Pts',(-20.3444477103439,-17.5778332269467,
2.39938689371169));
#160548=CARTESIAN_POINT('Ctrl Pts',(-20.3868894745888,-17.6282285501123,
2.39571801256821));
#160549=CARTESIAN_POINT('Ctrl Pts',(-20.4190315225978,-17.6693918689559,
2.3928615095606));
#160550=CARTESIAN_POINT('Ctrl Pts',(-20.5137302381864,-17.8003822313344,
2.38406095003522));
#160551=CARTESIAN_POINT('Ctrl Pts',(-20.5708677379246,-17.8938982825623,
2.37816909391497));
#160552=CARTESIAN_POINT('Ctrl Pts',(-20.6549212452758,-18.0589719937411,
2.36786978230487));
#160553=CARTESIAN_POINT('Ctrl Pts',(-20.6856664674143,-18.1283291310996,
2.36357214980944));
#160554=CARTESIAN_POINT('Ctrl Pts',(-20.7160027874429,-18.2080616742,2.35859161515212));
#160555=CARTESIAN_POINT('Ctrl Pts',(-20.7193217417052,-18.2169647250411,
2.35803497993091));
#160556=CARTESIAN_POINT('Ctrl Pts',(-20.7225805738064,-18.2258896079247,
2.35747639166834));
#160557=CARTESIAN_POINT('',(-20.849962012661,-18.9501158126703,2.8890562790225));
#160558=CARTESIAN_POINT('Ctrl Pts',(-20.849962012661,-18.9501158126703,
2.8890562790225));
#160559=CARTESIAN_POINT('Ctrl Pts',(-20.8456331599479,-19.4559949671801,
2.85866010167885));
#160560=CARTESIAN_POINT('Ctrl Pts',(-20.410193517051,-20.6740880447519,
2.78587198877475));
#160561=CARTESIAN_POINT('Ctrl Pts',(-18.3741968385222,-21.4292710094645,
2.67069194031011));
#160562=CARTESIAN_POINT('Ctrl Pts',(-16.4562524857842,-19.9903623098931,
2.54351613362868));
#160563=CARTESIAN_POINT('Ctrl Pts',(-16.6280001024638,-17.5988205946497,
2.41634032694725));
#160564=CARTESIAN_POINT('Ctrl Pts',(-18.7318719157381,-16.448737081536,
2.28916452026583));
#160565=CARTESIAN_POINT('Ctrl Pts',(-20.2929104264445,-17.2986361211697,
2.19488963603122));
#160566=CARTESIAN_POINT('Ctrl Pts',(-20.670180409037,-18.0771167134768,
2.1430066873571));
#160567=CARTESIAN_POINT('Ctrl Pts',(-20.7227693997001,-18.2258206865925,
2.13351567424346));
#160568=CARTESIAN_POINT('Ctrl Pts',(-20.8509991255275,-18.9500758077574,
2.88845974797779));
#160569=CARTESIAN_POINT('Ctrl Pts',(-20.850857410614,-18.7941608522463,
2.89867443023815));
#160570=CARTESIAN_POINT('Ctrl Pts',(-20.8334923215512,-18.6387336577071,
2.90915374483203));
#160571=CARTESIAN_POINT('Ctrl Pts',(-20.7924732127667,-18.456705003608,
2.92098938639697));
#160572=CARTESIAN_POINT('Ctrl Pts',(-20.7850834951854,-18.4269420749175,
2.9229085845561));
#160573=CARTESIAN_POINT('Ctrl Pts',(-20.7751867696799,-18.3904876570822,
2.92523075559935));
#160574=CARTESIAN_POINT('Ctrl Pts',(-20.7732896035714,-18.3836361587522,
2.92566594769897));
#160575=CARTESIAN_POINT('Ctrl Pts',(-20.7702491090473,-18.3728668375536,
2.92634787332317));
#160576=CARTESIAN_POINT('Ctrl Pts',(-20.7691289247223,-18.3689426148742,
2.92659591554719));
#160577=CARTESIAN_POINT('Ctrl Pts',(-20.7670057657387,-18.3615854447296,
2.92706008118862));
#160578=CARTESIAN_POINT('Ctrl Pts',(-20.7660054511583,-18.3581518398861,
2.92727634930289));
#160579=CARTESIAN_POINT('Ctrl Pts',(-20.7636912486175,-18.3502825948929,
2.92777119465781));
#160580=CARTESIAN_POINT('Ctrl Pts',(-20.7623715216973,-18.3458487224942,
2.92804942769785));
#160581=CARTESIAN_POINT('Ctrl Pts',(-20.7588689785161,-18.3342208018338,
2.92877765083969));
#160582=CARTESIAN_POINT('Ctrl Pts',(-20.7566623348027,-18.3270339201095,
2.92922628571805));
#160583=CARTESIAN_POINT('Ctrl Pts',(-20.7445408458542,-18.288291834689,
2.93163759997949));
#160584=CARTESIAN_POINT('Ctrl Pts',(-20.733925666785,-18.2569601334749,
2.93356211485035));
#160585=CARTESIAN_POINT('Ctrl Pts',(-20.7225805736403,-18.2258896074698,
2.9354567758078));
#160586=CARTESIAN_POINT('Origin',(-18.734,-18.952,0.));
#160587=CARTESIAN_POINT('',(-20.722580643286,-18.2258897982069,3.95421663535642));
#160588=CARTESIAN_POINT('',(-20.7225805737618,-18.2258896078024,3.73234499902338));
#160589=CARTESIAN_POINT('',(-20.7225805737622,-18.2258896078036,0.));
#160590=CARTESIAN_POINT('Ctrl Pts',(-20.722580643286,-18.2258897982069,
3.95421663535643));
#160591=CARTESIAN_POINT('Ctrl Pts',(-20.7432514728671,-18.2825005047965,
3.95029637644732));
#160592=CARTESIAN_POINT('Ctrl Pts',(-20.7615069693432,-18.339999464268,
3.94643464604714));
#160593=CARTESIAN_POINT('Ctrl Pts',(-20.7804090246118,-18.4097441966995,
3.94195346478622));
#160594=CARTESIAN_POINT('Ctrl Pts',(-20.7834316360229,-18.4212823382214,
3.9412186908867));
#160595=CARTESIAN_POINT('Ctrl Pts',(-20.7875891299676,-18.4377180308393,
3.94018194661357));
#160596=CARTESIAN_POINT('Ctrl Pts',(-20.7888042694118,-18.4425947839614,
3.93987556277719));
#160597=CARTESIAN_POINT('Ctrl Pts',(-20.7908681043649,-18.4510051823497,
3.93934935986463));
#160598=CARTESIAN_POINT('Ctrl Pts',(-20.7917250853805,-18.4545367552864,
3.93912906692465));
#160599=CARTESIAN_POINT('Ctrl Pts',(-20.793368805131,-18.4613873637551,
3.93870304221645));
#160600=CARTESIAN_POINT('Ctrl Pts',(-20.7941566162606,-18.4647060935657,
3.93849724659215));
#160601=CARTESIAN_POINT('Ctrl Pts',(-20.7962599600511,-18.4736629061791,
3.93794338394597));
#160602=CARTESIAN_POINT('Ctrl Pts',(-20.7975604024717,-18.4793045533346,
3.93759617847265));
#160603=CARTESIAN_POINT('Ctrl Pts',(-20.8022980768258,-18.5002499786051,
3.93631303011186));
#160604=CARTESIAN_POINT('Ctrl Pts',(-20.8055884395398,-18.5155869088825,
3.93538513345564));
#160605=CARTESIAN_POINT('Ctrl Pts',(-20.8354454606658,-18.6627095824125,
3.92658321823459));
#160606=CARTESIAN_POINT('Ctrl Pts',(-20.8495760231323,-18.7967260298796,
3.91931208592608));
#160607=CARTESIAN_POINT('Ctrl Pts',(-20.8509595378659,-18.9374794217699,
3.91166815891939));
#160608=CARTESIAN_POINT('Ctrl Pts',(-20.8509933270794,-18.9437668212733,
3.91132672589034));
#160609=CARTESIAN_POINT('Ctrl Pts',(-20.8511331452923,-19.0958927699035,
3.90306449741813));
#160610=CARTESIAN_POINT('Ctrl Pts',(-20.8361978944804,-19.2413359766959,
3.8951037815209));
#160611=CARTESIAN_POINT('Ctrl Pts',(-20.8015323044882,-19.4076057123349,
3.88524452288232));
#160612=CARTESIAN_POINT('Ctrl Pts',(-20.7962279547766,-19.4310429922329,
3.88383774041166));
#160613=CARTESIAN_POINT('Ctrl Pts',(-20.7882195556456,-19.4638256313104,
3.88184401110845));
#160614=CARTESIAN_POINT('Ctrl Pts',(-20.7858481757337,-19.4732509171373,
3.88126775903198));
#160615=CARTESIAN_POINT('Ctrl Pts',(-20.7819083814074,-19.4884664423229,
3.88033245111997));
#160616=CARTESIAN_POINT('Ctrl Pts',(-20.7803800925229,-19.4942669989618,
3.87997469653568));
#160617=CARTESIAN_POINT('Ctrl Pts',(-20.7771446747113,-19.5063384126534,
3.87922766363171));
#160618=CARTESIAN_POINT('Ctrl Pts',(-20.7754332825869,-19.5126080527688,
3.87883825025342));
#160619=CARTESIAN_POINT('Ctrl Pts',(-20.7713216387836,-19.5274024436891,
3.87791595248192));
#160620=CARTESIAN_POINT('Ctrl Pts',(-20.7688967234845,-19.5359201598563,
3.8773822701327));
#160621=CARTESIAN_POINT('Ctrl Pts',(-20.7606830657947,-19.564098689347,
3.87560769559069));
#160622=CARTESIAN_POINT('Ctrl Pts',(-20.7546623993838,-19.5836901740856,
3.87435926264209));
#160623=CARTESIAN_POINT('Ctrl Pts',(-20.7212770166753,-19.6869627376828,
3.86769856750041));
#160624=CARTESIAN_POINT('Ctrl Pts',(-20.6889997166902,-19.7689534180585,
3.86212565012843));
#160625=CARTESIAN_POINT('Ctrl Pts',(-20.596895197613,-19.9659340688863,
3.84804789280976));
#160626=CARTESIAN_POINT('Ctrl Pts',(-20.531438235175,-20.0779009529177,
3.83941397487547));
#160627=CARTESIAN_POINT('Ctrl Pts',(-20.4404280187582,-20.2052061074316,
3.82914932405589));
#160628=CARTESIAN_POINT('Ctrl Pts',(-20.4242597092025,-20.2269291436962,
3.82738151409786));
#160629=CARTESIAN_POINT('Ctrl Pts',(-20.3725012453261,-20.2937536422861,
3.82190467509247));
#160630=CARTESIAN_POINT('Ctrl Pts',(-20.3354861302741,-20.3377245765649,
3.81824387044658));
#160631=CARTESIAN_POINT('Ctrl Pts',(-20.2907366205742,-20.3866912153627,
3.81415065877349));
#160632=CARTESIAN_POINT('Ctrl Pts',(-20.2847073304121,-20.393205943303,
3.81360573899493));
#160633=CARTESIAN_POINT('Ctrl Pts',(-20.2755484457244,-20.4029782182891,
3.81278809120708));
#160634=CARTESIAN_POINT('Ctrl Pts',(-20.2724491963512,-20.4062638933788,
3.81251313465858));
#160635=CARTESIAN_POINT('Ctrl Pts',(-20.2668840549586,-20.4121260878752,
3.81202252978854));
#160636=CARTESIAN_POINT('Ctrl Pts',(-20.2644221547996,-20.41470630926,3.81180658179284));
#160637=CARTESIAN_POINT('Ctrl Pts',(-20.2590780366655,-20.4202790073261,
3.81134016612265));
#160638=CARTESIAN_POINT('Ctrl Pts',(-20.2561935353685,-20.4232692149426,
3.81108988037117));
#160639=CARTESIAN_POINT('Ctrl Pts',(-20.2481155994519,-20.4315939916044,
3.81039297116676));
#160640=CARTESIAN_POINT('Ctrl Pts',(-20.2429027405549,-20.4369097453308,
3.80994783512988));
#160641=CARTESIAN_POINT('Ctrl Pts',(-20.2125450870429,-20.4675416790893,
3.80738120982499));
#160642=CARTESIAN_POINT('Ctrl Pts',(-20.1867898930599,-20.4922480389433,
3.80530493917686));
#160643=CARTESIAN_POINT('Ctrl Pts',(-20.102148917991,-20.5694290007856,
3.79875037057054));
#160644=CARTESIAN_POINT('Ctrl Pts',(-20.0409487441668,-20.6192717091496,
3.79440913065695));
#160645=CARTESIAN_POINT('Ctrl Pts',(-19.9033750794258,-20.7190732835977,
3.78513986639871));
#160646=CARTESIAN_POINT('Ctrl Pts',(-19.8262702742676,-20.7677454640115,
3.78023284397057));
#160647=CARTESIAN_POINT('Ctrl Pts',(-19.652946817895,-20.8621090647309,
3.76938681059503));
#160648=CARTESIAN_POINT('Ctrl Pts',(-19.5559418736567,-20.9058135002402,
3.76342391385564));
#160649=CARTESIAN_POINT('Ctrl Pts',(-19.4428147572125,-20.9468607962405,
3.75637205774369));
#160650=CARTESIAN_POINT('Ctrl Pts',(-19.4295079082076,-20.9515391198206,
3.75554127869965));
#160651=CARTESIAN_POINT('Ctrl Pts',(-19.4082025843455,-20.9587910835033,
3.75420866601462));
#160652=CARTESIAN_POINT('Ctrl Pts',(-19.4002336772001,-20.9614507363524,
3.75370967776368));
#160653=CARTESIAN_POINT('Ctrl Pts',(-19.3861207167785,-20.966067811507,
3.75282491846104));
#160654=CARTESIAN_POINT('Ctrl Pts',(-19.3799831214154,-20.9680447376055,
3.75243979584654));
#160655=CARTESIAN_POINT('Ctrl Pts',(-19.3672398389072,-20.9720851960019,
3.75163941531339));
#160656=CARTESIAN_POINT('Ctrl Pts',(-19.3606328812423,-20.9741444367458,
3.75122402171573));
#160657=CARTESIAN_POINT('Ctrl Pts',(-19.3435841332429,-20.9793665723546,
3.75015098425139));
#160658=CARTESIAN_POINT('Ctrl Pts',(-19.3331278717998,-20.9824811795375,
3.74949176897933));
#160659=CARTESIAN_POINT('Ctrl Pts',(-19.2888354802327,-20.9953026425409,
3.74669438777854));
#160660=CARTESIAN_POINT('Ctrl Pts',(-19.2547856627965,-21.0042451508037,
3.74453156281268));
#160661=CARTESIAN_POINT('Ctrl Pts',(-19.1649577346654,-21.0254572458716,
3.73879018072131));
#160662=CARTESIAN_POINT('Ctrl Pts',(-19.1088812955984,-21.0363254608735,
3.73516993976684));
#160663=CARTESIAN_POINT('Ctrl Pts',(-18.9020664741558,-21.0677924445843,
3.72170210646169));
#160664=CARTESIAN_POINT('Ctrl Pts',(-18.7496716503156,-21.0743976122479,
3.71151603661502));
#160665=CARTESIAN_POINT('Ctrl Pts',(-18.5754032553887,-21.0631713745418,
3.70010994012028));
#160666=CARTESIAN_POINT('Ctrl Pts',(-18.5529239777217,-21.0613622317525,
3.69864423533809));
#160667=CARTESIAN_POINT('Ctrl Pts',(-18.4793791975006,-21.0542589343253,
3.69387531243316));
#160668=CARTESIAN_POINT('Ctrl Pts',(-18.428472714133,-21.0474661518653,
3.6906158705154));
#160669=CARTESIAN_POINT('Ctrl Pts',(-18.3700968251107,-21.0375036543208,
3.686963342813));
#160670=CARTESIAN_POINT('Ctrl Pts',(-18.3623415456984,-21.036135554764,
3.68647985595929));
#160671=CARTESIAN_POINT('Ctrl Pts',(-18.3499881034836,-21.0338851507914,
3.68571270205638));
#160672=CARTESIAN_POINT('Ctrl Pts',(-18.3453850076152,-21.0330308278389,
3.68542751260689));
#160673=CARTESIAN_POINT('Ctrl Pts',(-18.3372543307682,-21.031493876656,
3.68492499000434));
#160674=CARTESIAN_POINT('Ctrl Pts',(-18.3337256055918,-21.0308175290372,
3.68470730329842));
#160675=CARTESIAN_POINT('Ctrl Pts',(-18.3262686046166,-21.0293685606493,
3.68424816104702));
#160676=CARTESIAN_POINT('Ctrl Pts',(-18.3223408008086,-21.0285937811447,
3.68400683019085));
#160677=CARTESIAN_POINT('Ctrl Pts',(-18.3117869240203,-21.0264808539004,
3.68335970160561));
#160678=CARTESIAN_POINT('Ctrl Pts',(-18.305164958688,-21.025122091168,3.68295506454354));
#160679=CARTESIAN_POINT('Ctrl Pts',(-18.2728516921507,-21.0183302714414,
3.6809868957532));
#160680=CARTESIAN_POINT('Ctrl Pts',(-18.2472552510869,-21.0124509809377,
3.67944745098241));
#160681=CARTESIAN_POINT('Ctrl Pts',(-18.1742405819998,-20.9942434414176,
3.67509535991703));
#160682=CARTESIAN_POINT('Ctrl Pts',(-18.1271301565414,-20.9807430849332,
3.67233501553222));
#160683=CARTESIAN_POINT('Ctrl Pts',(-17.9886450523871,-20.9358010394224,
3.6642513840977));
#160684=CARTESIAN_POINT('Ctrl Pts',(-17.8989076960573,-20.8997276132652,
3.65904957781845));
#160685=CARTESIAN_POINT('Ctrl Pts',(-17.6849926586906,-20.7962241369201,
3.64611851301049));
#160686=CARTESIAN_POINT('Ctrl Pts',(-17.5645144196338,-20.7222754066084,
3.63833946390108));
#160687=CARTESIAN_POINT('Ctrl Pts',(-17.4409213804632,-20.628257942425,
3.62924206006671));
#160688=CARTESIAN_POINT('Ctrl Pts',(-17.4296416124583,-20.6194957834451,
3.62840094930856));
#160689=CARTESIAN_POINT('Ctrl Pts',(-17.411829060187,-20.6053676102057,
3.62705488629684));
#160690=CARTESIAN_POINT('Ctrl Pts',(-17.4052381398353,-20.6000753515461,
3.62655287166917));
#160691=CARTESIAN_POINT('Ctrl Pts',(-17.3936690618374,-20.5906713101343,
3.62566459434516));
#160692=CARTESIAN_POINT('Ctrl Pts',(-17.3886776615513,-20.5865759360453,
3.62527899702558));
#160693=CARTESIAN_POINT('Ctrl Pts',(-17.3783916972999,-20.5780574177055,
3.62447944953752));
#160694=CARTESIAN_POINT('Ctrl Pts',(-17.3730998703272,-20.5736311021093,
3.62406537266661));
#160695=CARTESIAN_POINT('Ctrl Pts',(-17.3595700481087,-20.562201298001,
3.6229995851441));
#160696=CARTESIAN_POINT('Ctrl Pts',(-17.3513639766922,-20.5551604826089,
3.62234634345402));
#160697=CARTESIAN_POINT('Ctrl Pts',(-17.3173225602285,-20.5254971458285,
3.6196075126603));
#160698=CARTESIAN_POINT('Ctrl Pts',(-17.2919868361175,-20.5023115991706,
3.61749853309025));
#160699=CARTESIAN_POINT('Ctrl Pts',(-17.2274367227848,-20.4402879953586,
3.61193407543417));
#160700=CARTESIAN_POINT('Ctrl Pts',(-17.1891592080074,-20.4005165406864,
3.60844003970799));
#160701=CARTESIAN_POINT('Ctrl Pts',(-17.0797169735442,-20.2775255702836,
3.59785715484333));
#160702=CARTESIAN_POINT('Ctrl Pts',(-17.0134092598667,-20.1902384301811,
3.59061995961833));
#160703=CARTESIAN_POINT('Ctrl Pts',(-16.9253148622675,-20.0534462249615,
3.57987230278306));
#160704=CARTESIAN_POINT('Ctrl Pts',(-16.8981766621931,-20.0075940145309,
3.57636186681366));
#160705=CARTESIAN_POINT('Ctrl Pts',(-16.8669437743949,-19.9499683788807,
3.57209596865354));
#160706=CARTESIAN_POINT('Ctrl Pts',(-16.8611855458393,-19.9391199844147,
3.57129908728673));
#160707=CARTESIAN_POINT('Ctrl Pts',(-16.8307532799089,-19.8805612281633,
3.56703290106919));
#160708=CARTESIAN_POINT('Ctrl Pts',(-16.807805072,-19.8319705603094,3.56361766533237));
#160709=CARTESIAN_POINT('Ctrl Pts',(-16.7833021256937,-19.774522383476,
3.55976484314492));
#160710=CARTESIAN_POINT('Ctrl Pts',(-16.779925545335,-19.7664681085246,
3.55922881886242));
#160711=CARTESIAN_POINT('Ctrl Pts',(-16.7748900638979,-19.7542452133867,
3.55842187739812));
#160712=CARTESIAN_POINT('Ctrl Pts',(-16.7731944603826,-19.75009195009,3.55814881572958));
#160713=CARTESIAN_POINT('Ctrl Pts',(-16.7701754192076,-19.7426293181134,
3.55766024530236));
#160714=CARTESIAN_POINT('Ctrl Pts',(-16.7688471312163,-19.7393219834874,
3.55744444743217));
#160715=CARTESIAN_POINT('Ctrl Pts',(-16.7659800356315,-19.7321306763522,
3.55697681494913));
#160716=CARTESIAN_POINT('Ctrl Pts',(-16.7644443751468,-19.7282455111885,
3.55672517056206));
#160717=CARTESIAN_POINT('Ctrl Pts',(-16.7601655837186,-19.7173258813387,
3.55602063045228));
#160718=CARTESIAN_POINT('Ctrl Pts',(-16.7574485384548,-19.7102811690266,
3.55556927538782));
#160719=CARTESIAN_POINT('Ctrl Pts',(-16.7414798344364,-19.6682087151315,
3.5528917129827));
#160720=CARTESIAN_POINT('Ctrl Pts',(-16.7291209747682,-19.6328465439972,
3.55071541726821));
#160721=CARTESIAN_POINT('Ctrl Pts',(-16.6916345280616,-19.5156938909797,
3.54368991079821));
#160722=CARTESIAN_POINT('Ctrl Pts',(-16.6705236685077,-19.4327028859298,
3.53900142683909));
#160723=CARTESIAN_POINT('Ctrl Pts',(-16.6212212041362,-19.1742301047384,
3.52467922389372));
#160724=CARTESIAN_POINT('Ctrl Pts',(-16.6100300165562,-18.9963325385406,
3.51514288356901));
#160725=CARTESIAN_POINT('Ctrl Pts',(-16.6226068843731,-18.7963418021158,
3.50349692494253));
#160726=CARTESIAN_POINT('Ctrl Pts',(-16.6244085276511,-18.7735788034323,
3.50215907793698));
#160727=CARTESIAN_POINT('Ctrl Pts',(-16.6274825309702,-18.7413728710314,
3.50024707615929));
#160728=CARTESIAN_POINT('Ctrl Pts',(-16.6284510170359,-18.7319020431186,
3.49968246037292));
#160729=CARTESIAN_POINT('Ctrl Pts',(-16.6301298608119,-18.7165111789643,
3.49876096907981));
#160730=CARTESIAN_POINT('Ctrl Pts',(-16.6308014124554,-18.7105869770904,
3.49840531969327));
#160731=CARTESIAN_POINT('Ctrl Pts',(-16.632260750175,-18.698181657758,3.49765855872333));
#160732=CARTESIAN_POINT('Ctrl Pts',(-16.6330535090957,-18.6917011986428,
3.49726729380674));
#160733=CARTESIAN_POINT('Ctrl Pts',(-16.6350132414274,-18.6762736894393,
3.49633302656511));
#160734=CARTESIAN_POINT('Ctrl Pts',(-16.6362074555004,-18.6673302838364,
3.49578916890026));
#160735=CARTESIAN_POINT('Ctrl Pts',(-16.6404362606815,-18.637133723556,
3.49394509935626));
#160736=CARTESIAN_POINT('Ctrl Pts',(-16.6437368836376,-18.6159197213011,
3.49263651248547));
#160737=CARTESIAN_POINT('Ctrl Pts',(-16.663566812613,-18.5000929542532,
3.48541771865636));
#160738=CARTESIAN_POINT('Ctrl Pts',(-16.6861953527151,-18.4066511612053,
3.47931513402387));
#160739=CARTESIAN_POINT('Ctrl Pts',(-16.7650870666264,-18.1565801944211,
3.46226905562621));
#160740=CARTESIAN_POINT('Ctrl Pts',(-16.8335759838245,-18.0045315827241,
3.45106738850449));
#160741=CARTESIAN_POINT('Ctrl Pts',(-16.9396684084912,-17.82787670827,3.43788089264322));
#160742=CARTESIAN_POINT('Ctrl Pts',(-16.9611615172917,-17.7942767079831,
3.43536743624608));
#160743=CARTESIAN_POINT('Ctrl Pts',(-16.9877110953604,-17.7552470253852,
3.43245945649443));
#160744=CARTESIAN_POINT('Ctrl Pts',(-16.9918611276591,-17.7492137456033,
3.4320102771075));
#160745=CARTESIAN_POINT('Ctrl Pts',(-16.9986503136441,-17.7394525470838,
3.43128427022541));
#160746=CARTESIAN_POINT('Ctrl Pts',(-17.0012703326298,-17.7357114815031,
3.43100619411151));
#160747=CARTESIAN_POINT('Ctrl Pts',(-17.0059601534859,-17.7290609019435,
3.43051220280399));
#160748=CARTESIAN_POINT('Ctrl Pts',(-17.0080252242335,-17.7261481236463,
3.43029597059652));
#160749=CARTESIAN_POINT('Ctrl Pts',(-17.012488550928,-17.7198862479496,
3.42983138873855));
#160750=CARTESIAN_POINT('Ctrl Pts',(-17.0148892078344,-17.7165389313289,
3.42958320798276));
#160751=CARTESIAN_POINT('Ctrl Pts',(-17.0215612462194,-17.7072929853906,
3.42889807392807));
#160752=CARTESIAN_POINT('Ctrl Pts',(-17.0258533656066,-17.7014092929413,
3.42846252755563));
#160753=CARTESIAN_POINT('Ctrl Pts',(-17.0498476960858,-17.6688715496211,
3.42605563313317));
#160754=CARTESIAN_POINT('Ctrl Pts',(-17.0701445885662,-17.6426593075903,
3.42412317563175));
#160755=CARTESIAN_POINT('Ctrl Pts',(-17.1933224983162,-17.4910750445309,
3.41291600934311));
#160756=CARTESIAN_POINT('Ctrl Pts',(-17.3097283755013,-17.3773727908762,
3.40434324969878));
#160757=CARTESIAN_POINT('Ctrl Pts',(-17.53019955142,-17.2066766759561,3.38907799497855));
#160758=CARTESIAN_POINT('Ctrl Pts',(-17.6281403069352,-17.1430339619579,
3.38256719283861));
#160759=CARTESIAN_POINT('Ctrl Pts',(-17.74341911688,-17.0809993606864,3.37489826862499));
#160760=CARTESIAN_POINT('Ctrl Pts',(-17.7560917917587,-17.074344706932,
3.37405538593873));
#160761=CARTESIAN_POINT('Ctrl Pts',(-17.7763617445352,-17.0639614490771,
3.37270701731893));
#160762=CARTESIAN_POINT('Ctrl Pts',(-17.7839157175794,-17.0601489352417,
3.37220448496859));
#160763=CARTESIAN_POINT('Ctrl Pts',(-17.7972748870594,-17.053506711104,
3.37131560448397));
#160764=CARTESIAN_POINT('Ctrl Pts',(-17.8030705883863,-17.0506580701087,
3.3709299246297));
#160765=CARTESIAN_POINT('Ctrl Pts',(-17.8150813455728,-17.0448227525706,
3.37013051304489));
#160766=CARTESIAN_POINT('Ctrl Pts',(-17.8212981340723,-17.0418398368857,
3.36971665612542));
#160767=CARTESIAN_POINT('Ctrl Pts',(-17.8372858275956,-17.0342645508872,
3.36865208090128));
#160768=CARTESIAN_POINT('Ctrl Pts',(-17.8470774026002,-17.0297164987353,
3.36799983827224));
#160769=CARTESIAN_POINT('Ctrl Pts',(-17.888027971071,-17.0110750073758,
3.36527068179004));
#160770=CARTESIAN_POINT('Ctrl Pts',(-17.9194899568447,-16.9976633667579,
3.36317058361158));
#160771=CARTESIAN_POINT('Ctrl Pts',(-18.0022416603367,-16.9647332183681,
3.35763512514042));
#160772=CARTESIAN_POINT('Ctrl Pts',(-18.0539873532097,-16.9464373562018,
3.35416170633538));
#160773=CARTESIAN_POINT('Ctrl Pts',(-18.2106712570855,-16.8977993402981,
3.34361843543464));
#160774=CARTESIAN_POINT('Ctrl Pts',(-18.3173020021354,-16.873545614891,
3.33640010712851));
#160775=CARTESIAN_POINT('Ctrl Pts',(-18.4467302746063,-16.8544696521033,
3.32775770745692));
#160776=CARTESIAN_POINT('Ctrl Pts',(-18.4681900765824,-16.8516422797544,
3.32632908382537));
#160777=CARTESIAN_POINT('Ctrl Pts',(-18.5860808693032,-16.8379456910899,
3.31851423229807));
#160778=CARTESIAN_POINT('Ctrl Pts',(-18.6831402305345,-16.8333864352845,
3.31219743472277));
#160779=CARTESIAN_POINT('Ctrl Pts',(-18.789869722037,-16.8357151623011,
3.30560165576851));
#160780=CARTESIAN_POINT('Ctrl Pts',(-18.7995583334116,-16.8359931348803,
3.30500613287629));
#160781=CARTESIAN_POINT('Ctrl Pts',(-18.8138609603363,-16.8365018170762,
3.30413210329348));
#160782=CARTESIAN_POINT('Ctrl Pts',(-18.8184765188449,-16.8366810988323,
3.30385083233343));
#160783=CARTESIAN_POINT('Ctrl Pts',(-18.8266639404182,-16.8370259625489,
3.30335332946701));
#160784=CARTESIAN_POINT('Ctrl Pts',(-18.8302360041293,-16.8371854887167,
3.30313676283711));
#160785=CARTESIAN_POINT('Ctrl Pts',(-18.8378885350119,-16.8375466752888,
3.30267386013529));
#160786=CARTESIAN_POINT('Ctrl Pts',(-18.841968816306,-16.83775109662,3.30242768036104));
#160787=CARTESIAN_POINT('Ctrl Pts',(-18.8531677295385,-16.8383446643873,
3.30175369164198));
#160788=CARTESIAN_POINT('Ctrl Pts',(-18.8602851030168,-16.8387579642702,
3.30132721528465));
#160789=CARTESIAN_POINT('Ctrl Pts',(-18.8982760273659,-16.8411566866239,
3.29906013320382));
#160790=CARTESIAN_POINT('Ctrl Pts',(-18.9291070962337,-16.8437828491535,
3.29725329225451));
#160791=CARTESIAN_POINT('Ctrl Pts',(-19.0222559743602,-16.8537783352635,
3.29186470316022));
#160792=CARTESIAN_POINT('Ctrl Pts',(-19.0843169673968,-16.8632432324067,
3.28836982246393));
#160793=CARTESIAN_POINT('Ctrl Pts',(-19.1792931399587,-16.8820811414239,
3.28304854736592));
#160794=CARTESIAN_POINT('Ctrl Pts',(-19.2125520155061,-16.8895165204692,
3.28119047272072));
#160795=CARTESIAN_POINT('Ctrl Pts',(-19.4135711000635,-16.9395809904895,
3.26992286268552));
#160796=CARTESIAN_POINT('Ctrl Pts',(-19.5757407703526,-17.0018428716841,
3.26060614985132));
#160797=CARTESIAN_POINT('Ctrl Pts',(-19.7489514508732,-17.0940176975786,
3.24920663689869));
#160798=CARTESIAN_POINT('Ctrl Pts',(-19.7692030571273,-17.1052246340875,
3.2478508445953));
#160799=CARTESIAN_POINT('Ctrl Pts',(-19.7975724039737,-17.1215370684914,
3.24591702942949));
#160800=CARTESIAN_POINT('Ctrl Pts',(-19.8058458968547,-17.126369377193,
3.24534883649737));
#160801=CARTESIAN_POINT('Ctrl Pts',(-19.8192235376731,-17.1343051540565,
3.24442310390202));
#160802=CARTESIAN_POINT('Ctrl Pts',(-19.8243479137603,-17.1373743897096,
3.24406681329985));
#160803=CARTESIAN_POINT('Ctrl Pts',(-19.8349259928411,-17.143771095013,
3.24332780767733));
#160804=CARTESIAN_POINT('Ctrl Pts',(-19.8403777544357,-17.1471016434035,
3.24294498232711));
#160805=CARTESIAN_POINT('Ctrl Pts',(-19.8532206524236,-17.1550275802876,
3.24203847591952));
#160806=CARTESIAN_POINT('Ctrl Pts',(-19.860598648776,-17.1596439452331,
3.24151402463974));
#160807=CARTESIAN_POINT('Ctrl Pts',(-19.8761590769948,-17.1695140409634,
3.24040003327959));
#160808=CARTESIAN_POINT('Ctrl Pts',(-19.8843341771871,-17.1747789031278,
3.23981008691391));
#160809=CARTESIAN_POINT('Ctrl Pts',(-19.9510641806848,-17.2184071406053,
3.23495567788343));
#160810=CARTESIAN_POINT('Ctrl Pts',(-20.0077135852105,-17.2595930329532,
3.23058526770339));
#160811=CARTESIAN_POINT('Ctrl Pts',(-20.204160162884,-17.41787270299,3.21449467864826));
#160812=CARTESIAN_POINT('Ctrl Pts',(-20.3307340145016,-17.550092909698,
3.2022186384488));
#160813=CARTESIAN_POINT('Ctrl Pts',(-20.4746945688649,-17.7456254667022,
3.18645674799399));
#160814=CARTESIAN_POINT('Ctrl Pts',(-20.5084970030197,-17.7959208813146,
3.18259024483368));
#160815=CARTESIAN_POINT('Ctrl Pts',(-20.5447854385542,-17.8552658458411,
3.17829709609899));
#160816=CARTESIAN_POINT('Ctrl Pts',(-20.5494233970414,-17.862960236993,
3.17774549514192));
#160817=CARTESIAN_POINT('Ctrl Pts',(-20.556331044366,-17.8745868143683,
3.17691981671473));
#160818=CARTESIAN_POINT('Ctrl Pts',(-20.5586372279976,-17.8784970447523,
3.17664344662023));
#160819=CARTESIAN_POINT('Ctrl Pts',(-20.5627335848153,-17.8854939253556,
3.17615131277197));
#160820=CARTESIAN_POINT('Ctrl Pts',(-20.5645285437771,-17.8885777026366,
3.17593524148028));
#160821=CARTESIAN_POINT('Ctrl Pts',(-20.568388443538,-17.8952478231693,
3.175469681873));
#160822=CARTESIAN_POINT('Ctrl Pts',(-20.5704506616512,-17.8988356761564,
3.17522036948238));
#160823=CARTESIAN_POINT('Ctrl Pts',(-20.576156204574,-17.908829911938,3.1745289120667));
#160824=CARTESIAN_POINT('Ctrl Pts',(-20.5797766571047,-17.91524937888,3.17408821694127));
#160825=CARTESIAN_POINT('Ctrl Pts',(-20.600144166551,-17.9518081301121,
3.17159718489627));
#160826=CARTESIAN_POINT('Ctrl Pts',(-20.6161875052244,-17.9823359703258,
3.1695890088521));
#160827=CARTESIAN_POINT('Ctrl Pts',(-20.6645332732958,-18.0800558020181,
3.16334241150832));
#160828=CARTESIAN_POINT('Ctrl Pts',(-20.6940384747307,-18.148572161805,
3.15922662494613));
#160829=CARTESIAN_POINT('Ctrl Pts',(-20.7207777061902,-18.220966334771,
3.15501082377172));
#160830=CARTESIAN_POINT('Ctrl Pts',(-20.7216814543783,-18.2234272117775,
3.15486767429015));
#160831=CARTESIAN_POINT('Ctrl Pts',(-20.7225805742799,-18.2258896092214,
3.15472458816501));
#160832=CARTESIAN_POINT('Ctrl Pts',(-20.7225805736403,-18.2258896074698,
2.9354567758078));
#160833=CARTESIAN_POINT('Ctrl Pts',(-20.7189843536169,-18.2160407286345,
2.93605735418876));
#160834=CARTESIAN_POINT('Ctrl Pts',(-20.7153147924264,-18.2062180923754,
2.93665493133054));
#160835=CARTESIAN_POINT('Ctrl Pts',(-20.6612838647028,-18.0648029998778,
2.94524329629832));
#160836=CARTESIAN_POINT('Ctrl Pts',(-20.5979773450729,-17.9385224517111,
2.95274653475215));
#160837=CARTESIAN_POINT('Ctrl Pts',(-20.4767571152221,-17.7470827157633,
2.965118514207));
#160838=CARTESIAN_POINT('Ctrl Pts',(-20.4265788956208,-17.6775577911004,
2.96985046744715));
#160839=CARTESIAN_POINT('Ctrl Pts',(-20.3428766244402,-17.5752763841308,
2.97737858817665));
#160840=CARTESIAN_POINT('Ctrl Pts',(-20.3122467006406,-17.5402674519987,
2.98006796802977));
#160841=CARTESIAN_POINT('Ctrl Pts',(-20.2724475184664,-17.4976936556449,
2.98349877117431));
#160842=CARTESIAN_POINT('Ctrl Pts',(-20.2643330904796,-17.4891574472824,
2.98419508992308));
#160843=CARTESIAN_POINT('Ctrl Pts',(-20.2511078907146,-17.4754752834189,
2.98532513730128));
#160844=CARTESIAN_POINT('Ctrl Pts',(-20.2460410921869,-17.4702870304024,
2.98575695145402));
#160845=CARTESIAN_POINT('Ctrl Pts',(-20.2364723931874,-17.4605891543958,
2.98657038829752));
#160846=CARTESIAN_POINT('Ctrl Pts',(-20.2319765851902,-17.4560736142701,
2.98695174024383));
#160847=CARTESIAN_POINT('Ctrl Pts',(-20.2218439581215,-17.4459879963035,
2.9878093996426));
#160848=CARTESIAN_POINT('Ctrl Pts',(-20.2161961337275,-17.4404291556478,
2.9882861949552));
#160849=CARTESIAN_POINT('Ctrl Pts',(-20.2017573966941,-17.4263766370199,
2.98950203354851));
#160850=CARTESIAN_POINT('Ctrl Pts',(-20.1929239736271,-17.417927234267,
2.99024298776385));
#160851=CARTESIAN_POINT('Ctrl Pts',(-20.1410560003854,-17.3691673156042,
2.99457763020889));
#160852=CARTESIAN_POINT('Ctrl Pts',(-20.0964291091927,-17.3305957500309,
2.99824448473656));
#160853=CARTESIAN_POINT('Ctrl Pts',(-20.0322504144338,-17.2796473889378,
3.00343722176584));
#160854=CARTESIAN_POINT('Ctrl Pts',(-20.0140157604129,-17.2656498016767,
3.00490392852665));
#160855=CARTESIAN_POINT('Ctrl Pts',(-19.8762572259285,-17.1634230950747,
3.01591749261086));
#160856=CARTESIAN_POINT('Ctrl Pts',(-19.747975118475,-17.0877022525259,
3.02584367188202));
#160857=CARTESIAN_POINT('Ctrl Pts',(-19.561180903465,-17.0024652853895,
3.03930122532286));
#160858=CARTESIAN_POINT('Ctrl Pts',(-19.5085863124353,-16.9809772237723,
3.04298513856761));
#160859=CARTESIAN_POINT('Ctrl Pts',(-19.4279314484675,-16.9517528654554,
3.04841761159787));
#160860=CARTESIAN_POINT('Ctrl Pts',(-19.4004733291517,-16.9424371245519,
3.05023006749216));
#160861=CARTESIAN_POINT('Ctrl Pts',(-19.3661731828607,-16.9315805301787,
3.05244118199199));
#160862=CARTESIAN_POINT('Ctrl Pts',(-19.3595048816588,-16.9295061401032,
3.05286858399254));
#160863=CARTESIAN_POINT('Ctrl Pts',(-19.3489502596895,-16.9262799784452,
3.05354105790895));
#160864=CARTESIAN_POINT('Ctrl Pts',(-19.345070755755,-16.9251063274758,
3.05378737986643));
#160865=CARTESIAN_POINT('Ctrl Pts',(-19.3377567865251,-16.922916568922,
3.05425012471986));
#160866=CARTESIAN_POINT('Ctrl Pts',(-19.3343231553902,-16.9218980476742,
3.05446668177415));
#160867=CARTESIAN_POINT('Ctrl Pts',(-19.3264786844876,-16.9195927773217,
3.05495988787756));
#160868=CARTESIAN_POINT('Ctrl Pts',(-19.3220662356164,-16.9183116724023,
3.05523620581616));
#160869=CARTESIAN_POINT('Ctrl Pts',(-19.3103651369411,-16.914955656489,
3.05596611322994));
#160870=CARTESIAN_POINT('Ctrl Pts',(-19.3030693813276,-16.9129054775131,
3.05641830172112));
#160871=CARTESIAN_POINT('Ctrl Pts',(-19.2525952298821,-16.8990137443759,
3.05952755652775));
#160872=CARTESIAN_POINT('Ctrl Pts',(-19.2090582999983,-16.8885044652083,
3.06211308673206));
#160873=CARTESIAN_POINT('Ctrl Pts',(-19.1583506230665,-16.8779544980118,
3.06504805793413));
#160874=CARTESIAN_POINT('Ctrl Pts',(-19.1514765912673,-16.8765599278267,
3.06544431710876));
#160875=CARTESIAN_POINT('Ctrl Pts',(-19.1224766395757,-16.8708264664554,
3.0671097274662));
#160876=CARTESIAN_POINT('Ctrl Pts',(-19.1002885778672,-16.8668069384044,
3.06836848375035));
#160877=CARTESIAN_POINT('Ctrl Pts',(-18.9305672089543,-16.8388534072115,
3.07790703647508));
#160878=CARTESIAN_POINT('Ctrl Pts',(-18.7809355827223,-16.8302490165657,
3.08583099852675));
#160879=CARTESIAN_POINT('Ctrl Pts',(-18.5728501230387,-16.8403219584417,
3.09738096150395));
#160880=CARTESIAN_POINT('Ctrl Pts',(-18.5142075431053,-16.8456182804935,
3.10069079874861));
#160881=CARTESIAN_POINT('Ctrl Pts',(-18.4201980566194,-16.8580774143171,
3.10613883521242));
#160882=CARTESIAN_POINT('Ctrl Pts',(-18.3846593851271,-16.8637125763828,
3.10823125268132));
#160883=CARTESIAN_POINT('Ctrl Pts',(-18.3384695212449,-16.872248676956,
3.11100070417082));
#160884=CARTESIAN_POINT('Ctrl Pts',(-18.3276719142188,-16.8743312571223,
3.1116516829094));
#160885=CARTESIAN_POINT('Ctrl Pts',(-18.3100877337299,-16.8778651088371,
3.11271784752408));
#160886=CARTESIAN_POINT('Ctrl Pts',(-18.3032911204841,-16.8792658116447,
3.1131314140681));
#160887=CARTESIAN_POINT('Ctrl Pts',(-18.2901994267912,-16.8820310291557,
3.11393092398268));
#160888=CARTESIAN_POINT('Ctrl Pts',(-18.2839034378841,-16.8833909087535,
3.11431671480448));
#160889=CARTESIAN_POINT('Ctrl Pts',(-18.2694533322152,-16.8865810999715,
3.11520517431173));
#160890=CARTESIAN_POINT('Ctrl Pts',(-18.2613036904933,-16.8884309958241,
3.11570846720079));
#160891=CARTESIAN_POINT('Ctrl Pts',(-18.2395758359834,-16.8934984904283,
3.11705631887774));
#160892=CARTESIAN_POINT('Ctrl Pts',(-18.226018298626,-16.8968021274566,
3.11790363290874));
#160893=CARTESIAN_POINT('Ctrl Pts',(-18.1162945233602,-16.9246911205168,
3.12481336577925));
#160894=CARTESIAN_POINT('Ctrl Pts',(-18.0219469884596,-16.9558745120497,
3.13109045023209));
#160895=CARTESIAN_POINT('Ctrl Pts',(-17.8032023036515,-17.0456595430858,
3.14642330491281));
#160896=CARTESIAN_POINT('Ctrl Pts',(-17.6816281939147,-17.1099825485712,
3.15560040410879));
#160897=CARTESIAN_POINT('Ctrl Pts',(-17.5252449601914,-17.2132872656533,
3.16784040676498));
#160898=CARTESIAN_POINT('Ctrl Pts',(-17.4843401028195,-17.2424499035351,
3.17108389014052));
#160899=CARTESIAN_POINT('Ctrl Pts',(-17.4233301878936,-17.2893073797455,
3.17594397430546));
#160900=CARTESIAN_POINT('Ctrl Pts',(-17.4024601395307,-17.3059733113391,
3.17761066245976));
#160901=CARTESIAN_POINT('Ctrl Pts',(-17.376679220801,-17.3273721925587,
3.17966896859267));
#160902=CARTESIAN_POINT('Ctrl Pts',(-17.3714693573658,-17.3317390762166,
3.18008488467663));
#160903=CARTESIAN_POINT('Ctrl Pts',(-17.3632183201068,-17.338722999153,
3.18074340955068));
#160904=CARTESIAN_POINT('Ctrl Pts',(-17.3601634470322,-17.3413236756751,
3.18098718390694));
#160905=CARTESIAN_POINT('Ctrl Pts',(-17.3543883840835,-17.3462684896978,
3.18144792088457));
#160906=CARTESIAN_POINT('Ctrl Pts',(-17.3516667996478,-17.3486108341045,
3.18166500181216));
#160907=CARTESIAN_POINT('Ctrl Pts',(-17.3454222998186,-17.3540129091287,
3.18216299237442));
#160908=CARTESIAN_POINT('Ctrl Pts',(-17.3419035333888,-17.3570773684487,
3.18244354741235));
#160909=CARTESIAN_POINT('Ctrl Pts',(-17.3325137043957,-17.3653096277068,
3.18319213288148));
#160910=CARTESIAN_POINT('Ctrl Pts',(-17.3266610369521,-17.3704984281846,
3.18365864546064));
#160911=CARTESIAN_POINT('Ctrl Pts',(-17.2835876265928,-17.4091144918838,
3.18709258576527));
#160912=CARTESIAN_POINT('Ctrl Pts',(-17.2475302829614,-17.4438221653688,
3.18997053400485));
#160913=CARTESIAN_POINT('Ctrl Pts',(-17.1954854466555,-17.4976007652329,
3.19419123180259));
#160914=CARTESIAN_POINT('Ctrl Pts',(-17.1785511370833,-17.515725977811,
3.19557589495216));
#160915=CARTESIAN_POINT('Ctrl Pts',(-17.1318547353183,-17.5675010916156,
3.19944012691856));
#160916=CARTESIAN_POINT('Ctrl Pts',(-17.1028390432233,-17.6018071130015,
3.20189612836868));
#160917=CARTESIAN_POINT('Ctrl Pts',(-17.0070173732553,-17.72270112243,3.21029482615913));
#160918=CARTESIAN_POINT('Ctrl Pts',(-16.9458402864307,-17.8135235278335,
3.2161825470462));
#160919=CARTESIAN_POINT('Ctrl Pts',(-16.8647983488402,-17.9566054534937,
3.22532602475029));
#160920=CARTESIAN_POINT('Ctrl Pts',(-16.839526304835,-18.0055889428265,
3.22843304907867));
#160921=CARTESIAN_POINT('Ctrl Pts',(-16.8016680748937,-18.0865757902056,
3.23357631824372));
#160922=CARTESIAN_POINT('Ctrl Pts',(-16.7878994557455,-18.1179986769741,
3.23557319031905));
#160923=CARTESIAN_POINT('Ctrl Pts',(-16.7708048958734,-18.1597432199516,
3.23823356323112));
#160924=CARTESIAN_POINT('Ctrl Pts',(-16.7667856448499,-18.1697765685351,
3.23887354193017));
#160925=CARTESIAN_POINT('Ctrl Pts',(-16.76032743814,-18.1862629681567,3.23992621484952));
#160926=CARTESIAN_POINT('Ctrl Pts',(-16.757842849447,-18.1926980192562,
3.24033736798002));
#160927=CARTESIAN_POINT('Ctrl Pts',(-16.75309356181,-18.2051798246134,3.24113543293024));
#160928=CARTESIAN_POINT('Ctrl Pts',(-16.7508249867812,-18.2112250296219,
3.24152220941669));
#160929=CARTESIAN_POINT('Ctrl Pts',(-16.7456497624845,-18.2252099204902,
3.24241760717204));
#160930=CARTESIAN_POINT('Ctrl Pts',(-16.7427629665166,-18.2331567904292,
3.24292688465869));
#160931=CARTESIAN_POINT('Ctrl Pts',(-16.7351250803477,-18.2545817008641,
3.24430126836301));
#160932=CARTESIAN_POINT('Ctrl Pts',(-16.7304627973821,-18.2680907294162,
3.24516930314691));
#160933=CARTESIAN_POINT('Ctrl Pts',(-16.6889155219294,-18.3925465770094,
3.25318084185257));
#160934=CARTESIAN_POINT('Ctrl Pts',(-16.6611499802037,-18.5063054517084,
3.26062649665945));
#160935=CARTESIAN_POINT('Ctrl Pts',(-16.6175000989483,-18.7826956361877,
3.27890436611869));
#160936=CARTESIAN_POINT('Ctrl Pts',(-16.6107477305492,-18.9460246569622,
3.28987716959584));
#160937=CARTESIAN_POINT('Ctrl Pts',(-16.6251785692284,-19.1406850008487,
3.30227739287311));
#160938=CARTESIAN_POINT('Ctrl Pts',(-16.6282990647217,-19.1728023788463,
3.30429910398492));
#160939=CARTESIAN_POINT('Ctrl Pts',(-16.6330153371594,-19.2120088745054,
3.3067273133095));
#160940=CARTESIAN_POINT('Ctrl Pts',(-16.6339146751838,-19.2191755981908,
3.30716954264857));
#160941=CARTESIAN_POINT('Ctrl Pts',(-16.6353827729412,-19.2304090394308,
3.30785999945032));
#160942=CARTESIAN_POINT('Ctrl Pts',(-16.6359267052709,-19.2344788656722,
3.30810958955294));
#160943=CARTESIAN_POINT('Ctrl Pts',(-16.6369660263569,-19.242086669096,
3.30857507365987));
#160944=CARTESIAN_POINT('Ctrl Pts',(-16.6374585242223,-19.2456249355406,
3.30879112174236));
#160945=CARTESIAN_POINT('Ctrl Pts',(-16.6386038540456,-19.2537035491606,
3.30928341475434));
#160946=CARTESIAN_POINT('Ctrl Pts',(-16.6392624862227,-19.2582430233319,
3.30955932862126));
#160947=CARTESIAN_POINT('Ctrl Pts',(-16.6413346149369,-19.2722051999186,
3.31040587146329));
#160948=CARTESIAN_POINT('Ctrl Pts',(-16.6427969970258,-19.2816206788458,
3.31097380747373));
#160949=CARTESIAN_POINT('Ctrl Pts',(-16.6634632591337,-19.4090026304001,
3.31862150857607));
#160950=CARTESIAN_POINT('Ctrl Pts',(-16.6925631239484,-19.5251645372952,
3.32518438122037));
#160951=CARTESIAN_POINT('Ctrl Pts',(-16.7897756523401,-19.8088544672473,
3.3415077460384));
#160952=CARTESIAN_POINT('Ctrl Pts',(-16.8697804148336,-19.9712577305101,
3.35119077557762));
#160953=CARTESIAN_POINT('Ctrl Pts',(-16.98128353714,-20.1394919427283,3.36294181459621));
#160954=CARTESIAN_POINT('Ctrl Pts',(-16.9934449610202,-20.1572469536441,
3.36420443967313));
#160955=CARTESIAN_POINT('Ctrl Pts',(-17.0110913380963,-20.1821854779148,
3.36601152113869));
#160956=CARTESIAN_POINT('Ctrl Pts',(-17.0163551176466,-20.1895243923299,
3.36654752159014));
#160957=CARTESIAN_POINT('Ctrl Pts',(-17.0255055982009,-20.2021114049617,
3.36747421490887));
#160958=CARTESIAN_POINT('Ctrl Pts',(-17.0293699478217,-20.2073756527556,
3.36786403902431));
#160959=CARTESIAN_POINT('Ctrl Pts',(-17.0368078309837,-20.2174103159717,
3.36861148471517));
#160960=CARTESIAN_POINT('Ctrl Pts',(-17.0403772806056,-20.2221836912667,
3.36896894439813));
#160961=CARTESIAN_POINT('Ctrl Pts',(-17.0496943817044,-20.2345342228267,
3.36989883371197));
#160962=CARTESIAN_POINT('Ctrl Pts',(-17.0554729727319,-20.2420877732378,
3.37047247748487));
#160963=CARTESIAN_POINT('Ctrl Pts',(-17.0752613334934,-20.2675963242239,
3.37242666728757));
#160964=CARTESIAN_POINT('Ctrl Pts',(-17.08950948013,-20.2853636107827,3.37381665733718));
#160965=CARTESIAN_POINT('Ctrl Pts',(-17.2178354197352,-20.4401985122437,
3.38619210787419));
#160966=CARTESIAN_POINT('Ctrl Pts',(-17.3485021423432,-20.5625467944461,
3.39790730800877));
#160967=CARTESIAN_POINT('Ctrl Pts',(-17.5618104034091,-20.7169058298442,
3.41530114228959));
#160968=CARTESIAN_POINT('Ctrl Pts',(-17.6336513022824,-20.7625677690027,
3.42090105858941));
#160969=CARTESIAN_POINT('Ctrl Pts',(-17.7406927695132,-20.8218723223083,
3.42871059508615));
#160970=CARTESIAN_POINT('Ctrl Pts',(-17.773812010481,-20.839093313998,3.43105731415141));
#160971=CARTESIAN_POINT('Ctrl Pts',(-17.8141533229791,-20.8587322790657,
3.43381811558067));
#160972=CARTESIAN_POINT('Ctrl Pts',(-17.8209528628771,-20.8619975975332,
3.43428017246368));
#160973=CARTESIAN_POINT('Ctrl Pts',(-17.8315438207849,-20.8670141731043,
3.43499462511591));
#160974=CARTESIAN_POINT('Ctrl Pts',(-17.8353231341563,-20.8687906328252,
3.43524854038106));
#160975=CARTESIAN_POINT('Ctrl Pts',(-17.8423378767047,-20.8720625932222,
3.43571788434527));
#160976=CARTESIAN_POINT('Ctrl Pts',(-17.8455717973452,-20.8735610927136,
3.4359334929003));
#160977=CARTESIAN_POINT('Ctrl Pts',(-17.8528865314438,-20.8769281022962,
3.43641945404905));
#160978=CARTESIAN_POINT('Ctrl Pts',(-17.8569695001643,-20.8787918015944,
3.43668950885962));
#160979=CARTESIAN_POINT('Ctrl Pts',(-17.8690236782532,-20.8842477600165,
3.43748334668969));
#160980=CARTESIAN_POINT('Ctrl Pts',(-17.8770113618401,-20.8878036892465,
3.43800495162242));
#160981=CARTESIAN_POINT('Ctrl Pts',(-17.9341712078765,-20.9128267677483,
3.44170760911095));
#160982=CARTESIAN_POINT('Ctrl Pts',(-17.9841261743647,-20.9324691340475,
3.44478611407843));
#160983=CARTESIAN_POINT('Ctrl Pts',(-18.0363416526327,-20.9507407473983,
3.44789636329138));
#160984=CARTESIAN_POINT('Ctrl Pts',(-18.037906110668,-20.9512861331552,
3.44798945300118));
#160985=CARTESIAN_POINT('Ctrl Pts',(-18.178835146446,-21.0002299373614,
3.45636641883946));
#160986=CARTESIAN_POINT('Ctrl Pts',(-18.322883395962,-21.0339324152017,
3.46418901548635));
#160987=CARTESIAN_POINT('Ctrl Pts',(-18.5662393653546,-21.0646043497105,
3.47766689188908));
#160988=CARTESIAN_POINT('Ctrl Pts',(-18.6639245256478,-21.0700951227057,
3.48313960275757));
#160989=CARTESIAN_POINT('Ctrl Pts',(-18.783299321396,-21.0685368170402,
3.49008940250181));
#160990=CARTESIAN_POINT('Ctrl Pts',(-18.8049596666604,-21.0679213585148,
3.49136060243591));
#160991=CARTESIAN_POINT('Ctrl Pts',(-18.8356538619996,-21.066577383287,
3.49317784822377));
#160992=CARTESIAN_POINT('Ctrl Pts',(-18.844698803562,-21.066123172518,3.49371530619552));
#160993=CARTESIAN_POINT('Ctrl Pts',(-18.8602649303925,-21.0652413191265,
3.49464372852697));
#160994=CARTESIAN_POINT('Ctrl Pts',(-18.8667876103792,-21.0648414882721,
3.49503381546947));
#160995=CARTESIAN_POINT('Ctrl Pts',(-18.879250753923,-21.0640195749745,
3.49578121673235));
#160996=CARTESIAN_POINT('Ctrl Pts',(-18.8851915012086,-21.063602613047,
3.49613836650912));
#160997=CARTESIAN_POINT('Ctrl Pts',(-18.9005867993991,-21.0624567652107,
3.49706625479941));
#160998=CARTESIAN_POINT('Ctrl Pts',(-18.9100382768923,-21.0616894179121,
3.49763819706302));
#160999=CARTESIAN_POINT('Ctrl Pts',(-18.9420026723806,-21.0588779970453,
3.49958040923052));
#161000=CARTESIAN_POINT('Ctrl Pts',(-18.9644872949331,-21.0565368970037,
3.50095996651489));
#161001=CARTESIAN_POINT('Ctrl Pts',(-19.1659644661462,-21.0322916634332,
3.51344598014439));
#161002=CARTESIAN_POINT('Ctrl Pts',(-19.3414810967892,-20.9879636674441,
3.52530090045895));
#161003=CARTESIAN_POINT('Ctrl Pts',(-19.5870795254064,-20.8913157871317,
3.54273401533952));
#161004=CARTESIAN_POINT('Ctrl Pts',(-19.66306218108,-20.8560839497504,3.54824056464897));
#161005=CARTESIAN_POINT('Ctrl Pts',(-19.7693191502955,-20.7989352124162,
3.55593787172297));
#161006=CARTESIAN_POINT('Ctrl Pts',(-19.8014125794361,-20.780574907359,
3.55826174865167));
#161007=CARTESIAN_POINT('Ctrl Pts',(-19.8394398714855,-20.7574772975466,
3.56099934003732));
#161008=CARTESIAN_POINT('Ctrl Pts',(-19.8458481690119,-20.7535380191362,
3.56146011403399));
#161009=CARTESIAN_POINT('Ctrl Pts',(-19.855777463325,-20.7473611680652,
3.56217301605454));
#161010=CARTESIAN_POINT('Ctrl Pts',(-19.8593129982942,-20.7451472492753,
3.56242665320708));
#161011=CARTESIAN_POINT('Ctrl Pts',(-19.8658576162719,-20.7410220913646,
3.56289574191379));
#161012=CARTESIAN_POINT('Ctrl Pts',(-19.8688683886892,-20.7391137198135,
3.5631113716836));
#161013=CARTESIAN_POINT('Ctrl Pts',(-19.8756641113796,-20.734782166603,
3.5635977078792));
#161014=CARTESIAN_POINT('Ctrl Pts',(-19.8794461640324,-20.7323545385483,
3.56386811451777));
#161015=CARTESIAN_POINT('Ctrl Pts',(-19.8905864468391,-20.7251536080428,
3.56466394647772));
#161016=CARTESIAN_POINT('Ctrl Pts',(-19.8979228802584,-20.7203465332218,
3.56518717733244));
#161017=CARTESIAN_POINT('Ctrl Pts',(-19.950759722872,-20.6852547976941,
3.56895082240495));
#161018=CARTESIAN_POINT('Ctrl Pts',(-19.9951061769294,-20.6532609195377,
3.57208474954758));
#161019=CARTESIAN_POINT('Ctrl Pts',(-20.1707488300931,-20.5158959470292,
3.58461108215611));
#161020=CARTESIAN_POINT('Ctrl Pts',(-20.2904968955431,-20.3967638835054,
3.59346953487657));
#161021=CARTESIAN_POINT('Ctrl Pts',(-20.4314207942789,-20.2184616133704,
3.60606882687358));
#161022=CARTESIAN_POINT('Ctrl Pts',(-20.466016053466,-20.1707214601449,
3.60938274878419));
#161023=CARTESIAN_POINT('Ctrl Pts',(-20.5184689858925,-20.0915860170233,
3.61483690256046));
#161024=CARTESIAN_POINT('Ctrl Pts',(-20.5375947524117,-20.0610678944997,
3.61693121802819));
#161025=CARTESIAN_POINT('Ctrl Pts',(-20.5615339674283,-20.0206110628523,
3.61970283292729));
#161026=CARTESIAN_POINT('Ctrl Pts',(-20.567061873677,-20.0111006402215,
3.62035402539116));
#161027=CARTESIAN_POINT('Ctrl Pts',(-20.5759561201111,-19.995520397025,
3.62142045227264));
#161028=CARTESIAN_POINT('Ctrl Pts',(-20.5793672167413,-19.9894762652877,
3.62183406582366));
#161029=CARTESIAN_POINT('Ctrl Pts',(-20.585886552817,-19.9777907588083,
3.62263360509031));
#161030=CARTESIAN_POINT('Ctrl Pts',(-20.588998892178,-19.9721517504557,
3.62301937792684));
#161031=CARTESIAN_POINT('Ctrl Pts',(-20.5960893372995,-19.9591653828508,
3.62390770805839));
#161032=CARTESIAN_POINT('Ctrl Pts',(-20.6000497574506,-19.9518085357159,
3.62441088895957));
#161033=CARTESIAN_POINT('Ctrl Pts',(-20.6105051153137,-19.932108206293,
3.62575824584063));
#161034=CARTESIAN_POINT('Ctrl Pts',(-20.6169217054464,-19.9197238141047,
3.62660517388026));
#161035=CARTESIAN_POINT('Ctrl Pts',(-20.667862316851,-19.8189805017949,
3.63349516038651));
#161036=CARTESIAN_POINT('Ctrl Pts',(-20.7062580256466,-19.7276752427533,
3.63975146334344));
#161037=CARTESIAN_POINT('Ctrl Pts',(-20.7819943072982,-19.5051266499831,
3.65499316859155));
#161038=CARTESIAN_POINT('Ctrl Pts',(-20.8133221629822,-19.3722922033889,
3.66409683868163));
#161039=CARTESIAN_POINT('Ctrl Pts',(-20.8417531160729,-19.1633140867206,
3.67787832339337));
#161040=CARTESIAN_POINT('Ctrl Pts',(-20.8479010495714,-19.0887540779393,
3.68268512141501));
#161041=CARTESIAN_POINT('Ctrl Pts',(-20.8503509139228,-19.0051628183103,
3.68784417170587));
#161042=CARTESIAN_POINT('Ctrl Pts',(-20.8505548518314,-18.9963062253306,
3.68838787831956));
#161043=CARTESIAN_POINT('Ctrl Pts',(-20.8507777608891,-18.9829958412862,
3.68920038145952));
#161044=CARTESIAN_POINT('Ctrl Pts',(-20.8508382797348,-18.9785429738362,
3.68947141983799));
#161045=CARTESIAN_POINT('Ctrl Pts',(-20.8509183444026,-18.9708703424099,
3.68993706203665));
#161046=CARTESIAN_POINT('Ctrl Pts',(-20.8509445960242,-18.9676507038288,
3.69013203820979));
#161047=CARTESIAN_POINT('Ctrl Pts',(-20.8509874023548,-18.9603608802205,
3.69057254223413));
#161048=CARTESIAN_POINT('Ctrl Pts',(-20.850999564596,-18.9562907096263,
3.69081782134309));
#161049=CARTESIAN_POINT('Ctrl Pts',(-20.8510007238669,-18.9451601480982,
3.69148680677765));
#161050=CARTESIAN_POINT('Ctrl Pts',(-20.8509661391287,-18.9380997334676,
3.69190921330968));
#161051=CARTESIAN_POINT('Ctrl Pts',(-20.8505991936736,-18.9010402233319,
3.69411677269202));
#161052=CARTESIAN_POINT('Ctrl Pts',(-20.8496644750514,-18.8710488854179,
3.69587022658714));
#161053=CARTESIAN_POINT('Ctrl Pts',(-20.8449576296193,-18.7813334830055,
3.70104316947266));
#161054=CARTESIAN_POINT('Ctrl Pts',(-20.8392906868578,-18.7217363983877,
3.70438375873542));
#161055=CARTESIAN_POINT('Ctrl Pts',(-20.8105320875148,-18.5134442303815,
3.71596092773406));
#161056=CARTESIAN_POINT('Ctrl Pts',(-20.7741426799691,-18.3671014728962,
3.723948917646));
#161057=CARTESIAN_POINT('Ctrl Pts',(-20.7225805737618,-18.2258896078024,
3.73234499902338));
#161058=CARTESIAN_POINT('Origin',(-18.734,-18.952,0.));
#161059=CARTESIAN_POINT('',(-20.7225805756119,-18.2258896128692,4.75730100916854));
#161060=CARTESIAN_POINT('',(-20.7225805465488,-18.2258895332749,4.53222344315201));
#161061=CARTESIAN_POINT('',(-20.7225805737622,-18.2258896078036,0.));
#161062=CARTESIAN_POINT('',(-20.8510004573069,-18.9525763811924,4.70909255089851));
#161063=CARTESIAN_POINT('Ctrl Pts',(-20.7225805756119,-18.2258896128692,
4.75730100916854));
#161064=CARTESIAN_POINT('Ctrl Pts',(-20.7394204630776,-18.2720085965712,
4.75422026792543));
#161065=CARTESIAN_POINT('Ctrl Pts',(-20.7546509859817,-18.3186997180878,
4.75109074222835));
#161066=CARTESIAN_POINT('Ctrl Pts',(-20.8232026681109,-18.556621319464,
4.73511031612701));
#161067=CARTESIAN_POINT('Ctrl Pts',(-20.8510537300821,-18.7541142038182,
4.72162174956493));
#161068=CARTESIAN_POINT('Ctrl Pts',(-20.8509999221896,-18.9525739767941,
4.70909177449283));
#161069=CARTESIAN_POINT('Ctrl Pts',(-20.8509999215522,-18.9525763226662,
4.70909162638368));
#161070=CARTESIAN_POINT('Ctrl Pts',(-20.8509956361641,-18.9683177933136,
4.70809777210637));
#161071=CARTESIAN_POINT('Ctrl Pts',(-20.8508157763218,-18.9840592918394,
4.70711104263526));
#161072=CARTESIAN_POINT('Ctrl Pts',(-20.8502148550793,-19.0106677173036,
4.70545679613841));
#161073=CARTESIAN_POINT('Ctrl Pts',(-20.8498856304571,-19.021535774254,
4.70478498365393));
#161074=CARTESIAN_POINT('Ctrl Pts',(-20.8492914998136,-19.0371682430673,
4.70382466716472));
#161075=CARTESIAN_POINT('Ctrl Pts',(-20.8490942019335,-19.041934847292,
4.70353265478901));
#161076=CARTESIAN_POINT('Ctrl Pts',(-20.8487208814591,-19.0502719292856,
4.70302336263931));
#161077=CARTESIAN_POINT('Ctrl Pts',(-20.8485519258392,-19.0538426822487,
4.70280570115822));
#161078=CARTESIAN_POINT('Ctrl Pts',(-20.8482044718395,-19.0608119131399,
4.70238181422817));
#161079=CARTESIAN_POINT('Ctrl Pts',(-20.8480268213021,-19.064210430191,
4.70217554205354));
#161080=CARTESIAN_POINT('Ctrl Pts',(-20.8476550554517,-19.0710079708271,
4.70176385304503));
#161081=CARTESIAN_POINT('Ctrl Pts',(-20.8474609360373,-19.0744069556023,
4.70155843620369));
#161082=CARTESIAN_POINT('Ctrl Pts',(-20.8469736816507,-19.0825917698856,
4.70106481870128));
#161083=CARTESIAN_POINT('Ctrl Pts',(-20.8466724839536,-19.0873771261272,
4.70077706715283));
#161084=CARTESIAN_POINT('Ctrl Pts',(-20.8455076200067,-19.1049326369219,
4.69972440335841));
#161085=CARTESIAN_POINT('Ctrl Pts',(-20.8445443860772,-19.1176962076478,
4.69896485939855));
#161086=CARTESIAN_POINT('Ctrl Pts',(-20.8412948277738,-19.1561092511592,
4.69669428548022));
#161087=CARTESIAN_POINT('Ctrl Pts',(-20.8386561572594,-19.1817273610097,
4.6952006328698));
#161088=CARTESIAN_POINT('Ctrl Pts',(-20.8126752036858,-19.395601144094,
4.68285649487282));
#161089=CARTESIAN_POINT('Ctrl Pts',(-20.7645928184162,-19.5799984010765,
4.67295994885061));
#161090=CARTESIAN_POINT('Ctrl Pts',(-20.6698522696631,-19.8109231607585,
4.65913210644751));
#161091=CARTESIAN_POINT('Ctrl Pts',(-20.6447914006982,-19.8653172694487,
4.65576807668629));
#161092=CARTESIAN_POINT('Ctrl Pts',(-20.6008326662732,-19.9509750429593,
4.6502389452701));
#161093=CARTESIAN_POINT('Ctrl Pts',(-20.5833720719599,-19.9829403697677,
4.64812142982974));
#161094=CARTESIAN_POINT('Ctrl Pts',(-20.5595535596603,-20.0239912249072,
4.64532338115277));
#161095=CARTESIAN_POINT('Ctrl Pts',(-20.5539360688136,-20.0335006629245,
4.64466959096941));
#161096=CARTESIAN_POINT('Ctrl Pts',(-20.5446628799948,-20.0489217103262,
4.64359997605349));
#161097=CARTESIAN_POINT('Ctrl Pts',(-20.5410519815476,-20.054860117055,
4.64318579088357));
#161098=CARTESIAN_POINT('Ctrl Pts',(-20.5340402940104,-20.0662645024054,
4.64238589126276));
#161099=CARTESIAN_POINT('Ctrl Pts',(-20.5306436819236,-20.0717329682412,
4.64200033369208));
#161100=CARTESIAN_POINT('Ctrl Pts',(-20.5227931860363,-20.0842443983085,
4.64111356041141));
#161101=CARTESIAN_POINT('Ctrl Pts',(-20.5183225750907,-20.0912766937104,
4.64061172828545));
#161102=CARTESIAN_POINT('Ctrl Pts',(-20.5062991728745,-20.1099451999045,
4.63927032576621));
#161103=CARTESIAN_POINT('Ctrl Pts',(-20.4986734230881,-20.1215337274407,
4.63842804148149));
#161104=CARTESIAN_POINT('Ctrl Pts',(-20.4373813341076,-20.2127123608421,
4.63172336173501));
#161105=CARTESIAN_POINT('Ctrl Pts',(-20.3784792952977,-20.2886327202349,
4.62566071632389));
#161106=CARTESIAN_POINT('Ctrl Pts',(-20.2144279288533,-20.4727611334893,
4.60969389042609));
#161107=CARTESIAN_POINT('Ctrl Pts',(-20.1025089562092,-20.5742083254242,
4.599590028446));
#161108=CARTESIAN_POINT('Ctrl Pts',(-19.9458032578401,-20.6884027855696,
4.58698689948742));
#161109=CARTESIAN_POINT('Ctrl Pts',(-19.9100533195716,-20.7128125479089,
4.5842058921462));
#161110=CARTESIAN_POINT('Ctrl Pts',(-19.8600571198533,-20.7447469892644,
4.58046833843027));
#161111=CARTESIAN_POINT('Ctrl Pts',(-19.8464379320344,-20.7532296591141,
4.57946513797292));
#161112=CARTESIAN_POINT('Ctrl Pts',(-19.8259213924213,-20.7656868510066,
4.57797755733392));
#161113=CARTESIAN_POINT('Ctrl Pts',(-19.8190962333495,-20.7697784489669,
4.57748655713292));
#161114=CARTESIAN_POINT('Ctrl Pts',(-19.8066052418891,-20.7771712220598,
4.57659521931768));
#161115=CARTESIAN_POINT('Ctrl Pts',(-19.8009468640458,-20.7804847242108,
4.5761941399543));
#161116=CARTESIAN_POINT('Ctrl Pts',(-19.7918811798887,-20.7857371066348,
4.57555594911289));
#161117=CARTESIAN_POINT('Ctrl Pts',(-19.7884837786593,-20.7876928741311,
4.57531776753106));
#161118=CARTESIAN_POINT('Ctrl Pts',(-19.7850704059233,-20.7896452328837,
4.57507946610141));
#161119=CARTESIAN_POINT('Ctrl Pts',(-19.7850598806106,-20.7896512529636,
4.57507873129605));
#161120=CARTESIAN_POINT('Ctrl Pts',(-19.7850387628336,-20.7896633312908,
4.57507725701638));
#161121=CARTESIAN_POINT('Ctrl Pts',(-19.7850281709602,-20.7896693891987,
4.57507651758343));
#161122=CARTESIAN_POINT('Ctrl Pts',(-19.785006899568,-20.7896815548981,
4.57507503261827));
#161123=CARTESIAN_POINT('Ctrl Pts',(-19.784996251202,-20.7896876448706,
4.57507428926086));
#161124=CARTESIAN_POINT('Ctrl Pts',(-19.7819654538141,-20.7914209720074,
4.57486271352688));
#161125=CARTESIAN_POINT('Ctrl Pts',(-19.7789410960357,-20.7931407362307,
4.57465237488139));
#161126=CARTESIAN_POINT('Ctrl Pts',(-19.7718898819355,-20.797127352347,
4.5741637849482));
#161127=CARTESIAN_POINT('Ctrl Pts',(-19.7678598345856,-20.7993884801959,
4.57388590307482));
#161128=CARTESIAN_POINT('Ctrl Pts',(-19.7571231115253,-20.8053663672551,
4.57314911936777));
#161129=CARTESIAN_POINT('Ctrl Pts',(-19.7504035211481,-20.8090599556381,
4.57269166101939));
#161130=CARTESIAN_POINT('Ctrl Pts',(-19.702691852327,-20.8349493031433,
4.56946829392327));
#161131=CARTESIAN_POINT('Ctrl Pts',(-19.6609932679525,-20.855824091235,
4.56677998671634));
#161132=CARTESIAN_POINT('Ctrl Pts',(-19.6064242874687,-20.8809234153024,
4.56338213954585));
#161133=CARTESIAN_POINT('Ctrl Pts',(-19.5941589960978,-20.8864239951325,
4.56262605861538));
#161134=CARTESIAN_POINT('Ctrl Pts',(-19.4323495090433,-20.9571469264488,
4.55274123491598));
#161135=CARTESIAN_POINT('Ctrl Pts',(-19.275800652933,-21.0049891365391,
4.54413717891616));
#161136=CARTESIAN_POINT('Ctrl Pts',(-19.0356857083949,-21.0489563911361,
4.53060672122021));
#161137=CARTESIAN_POINT('Ctrl Pts',(-18.9553060775102,-21.0589556061523,
4.52603185771475));
#161138=CARTESIAN_POINT('Ctrl Pts',(-18.855009070423,-21.0656294881102,
4.52016760183698));
#161139=CARTESIAN_POINT('Ctrl Pts',(-18.835444670874,-21.0666587783344,
4.51901658439269));
#161140=CARTESIAN_POINT('Ctrl Pts',(-18.8071792166809,-21.0677526869848,
4.51734234690472));
#161141=CARTESIAN_POINT('Ctrl Pts',(-18.7984872684684,-21.0680354484276,
4.51682595821711));
#161142=CARTESIAN_POINT('Ctrl Pts',(-18.7833241851723,-21.0684352131238,
4.51592233671));
#161143=CARTESIAN_POINT('Ctrl Pts',(-18.7768537560792,-21.0685761126754,
4.5155358577334));
#161144=CARTESIAN_POINT('Ctrl Pts',(-18.7643456771615,-21.0687911087188,
4.51478700380021));
#161145=CARTESIAN_POINT('Ctrl Pts',(-18.7583081497677,-21.068869049033,
4.51442475321397));
#161146=CARTESIAN_POINT('Ctrl Pts',(-18.7439645783304,-21.0689928434738,
4.51356223911529));
#161147=CARTESIAN_POINT('Ctrl Pts',(-18.7356584812932,-21.0690156443694,
4.51306125760957));
#161148=CARTESIAN_POINT('Ctrl Pts',(-18.7061860513453,-21.0689230996007,
4.51127813375996));
#161149=CARTESIAN_POINT('Ctrl Pts',(-18.6850223655456,-21.0685391953912,
4.50998762432205));
#161150=CARTESIAN_POINT('Ctrl Pts',(-18.4700720242088,-21.0614144662779,
4.49677402209619));
#161151=CARTESIAN_POINT('Ctrl Pts',(-18.2781107854518,-21.0283961381152,
4.48396670417523));
#161152=CARTESIAN_POINT('Ctrl Pts',(-18.0220320605073,-20.9470924163692,
4.46624541318947));
#161153=CARTESIAN_POINT('Ctrl Pts',(-17.9519342183132,-20.9206713155592,
4.46133988176395));
#161154=CARTESIAN_POINT('Ctrl Pts',(-17.8517247269387,-20.8767010855841,
4.45437312319282));
#161155=CARTESIAN_POINT('Ctrl Pts',(-17.8204129689883,-20.8620374295146,
4.45220348673806));
#161156=CARTESIAN_POINT('Ctrl Pts',(-17.7828717150715,-20.8433218613853,
4.44962325556869));
#161157=CARTESIAN_POINT('Ctrl Pts',(-17.7762881444837,-20.8399966639886,
4.44917156489774));
#161158=CARTESIAN_POINT('Ctrl Pts',(-17.7660368544956,-20.834751572612,
4.44846964984388));
#161159=CARTESIAN_POINT('Ctrl Pts',(-17.7623572346028,-20.8328552502403,
4.44821798887171));
#161160=CARTESIAN_POINT('Ctrl Pts',(-17.7555163688688,-20.8293043211756,
4.447750686974));
#161161=CARTESIAN_POINT('Ctrl Pts',(-17.7523537758621,-20.827652532211,
4.44753487955362));
#161162=CARTESIAN_POINT('Ctrl Pts',(-17.7451783526409,-20.8238817648832,
4.44704575592972));
#161163=CARTESIAN_POINT('Ctrl Pts',(-17.741168159685,-20.8217578799741,
4.44677275426929));
#161164=CARTESIAN_POINT('Ctrl Pts',(-17.7307902425689,-20.8162187086294,
4.44606710972104));
#161165=CARTESIAN_POINT('Ctrl Pts',(-17.7244330589556,-20.8127836537179,
4.44563568918966));
#161166=CARTESIAN_POINT('Ctrl Pts',(-17.6845977067841,-20.7909946891815,
4.44293679688666));
#161167=CARTESIAN_POINT('Ctrl Pts',(-17.651601309818,-20.7717692497599,
4.44072115258957));
#161168=CARTESIAN_POINT('Ctrl Pts',(-17.6086601237746,-20.7451679121406,
4.43784016549691));
#161169=CARTESIAN_POINT('Ctrl Pts',(-17.5982361918938,-20.7385837738038,
4.43714100626698));
#161170=CARTESIAN_POINT('Ctrl Pts',(-17.5823406566037,-20.7283482233389,
4.4360742271592));
#161171=CARTESIAN_POINT('Ctrl Pts',(-17.576827693612,-20.7247618307421,
4.43570412526519));
#161172=CARTESIAN_POINT('Ctrl Pts',(-17.4333767608454,-20.6304872335884,
4.42606839797569));
#161173=CARTESIAN_POINT('Ctrl Pts',(-17.3064941032793,-20.5239968610187,
4.41736987188445));
#161174=CARTESIAN_POINT('Ctrl Pts',(-17.1366846938526,-20.3437903046219,
4.40365776898426));
#161175=CARTESIAN_POINT('Ctrl Pts',(-17.0836655695203,-20.2804918285709,
4.39899842308611));
#161176=CARTESIAN_POINT('Ctrl Pts',(-17.0226760480942,-20.1983751990404,
4.39303223611609));
#161177=CARTESIAN_POINT('Ctrl Pts',(-17.0110975491467,-20.18232024722,4.39186946064101));
#161178=CARTESIAN_POINT('Ctrl Pts',(-16.9947378607424,-20.1589517277808,
4.39018117846389));
#161179=CARTESIAN_POINT('Ctrl Pts',(-16.9897739320065,-20.1517669284059,
4.38966266617503));
#161180=CARTESIAN_POINT('Ctrl Pts',(-16.9812054617203,-20.1391993391955,
4.3887565658211));
#161181=CARTESIAN_POINT('Ctrl Pts',(-16.9775808862501,-20.1338303007725,
4.38836974389897));
#161182=CARTESIAN_POINT('Ctrl Pts',(-16.9706308489813,-20.12343270472,4.38762112295267));
#161183=CARTESIAN_POINT('Ctrl Pts',(-16.9673021086385,-20.1184064059932,
4.38725945254638));
#161184=CARTESIAN_POINT('Ctrl Pts',(-16.9594582251438,-20.1064517648688,
4.38639973500791));
#161185=CARTESIAN_POINT('Ctrl Pts',(-16.9549621448496,-20.0995110871035,
4.38590098073955));
#161186=CARTESIAN_POINT('Ctrl Pts',(-16.9392200408535,-20.0748948285133,
4.38413330124108));
#161187=CARTESIAN_POINT('Ctrl Pts',(-16.9281961306753,-20.057079288413,
4.38285619663186));
#161188=CARTESIAN_POINT('Ctrl Pts',(-16.8170198525766,-19.8713025817194,
4.36955749566356));
#161189=CARTESIAN_POINT('Ctrl Pts',(-16.7403537964452,-19.6904257909128,
4.35663410099709));
#161190=CARTESIAN_POINT('Ctrl Pts',(-16.6623492899738,-19.4002960903783,
4.33682265673636));
#161191=CARTESIAN_POINT('Ctrl Pts',(-16.6426696297756,-19.2970342340231,
4.32996620057552));
#161192=CARTESIAN_POINT('Ctrl Pts',(-16.629677361173,-19.1835192046731,
4.32291230438946));
#161193=CARTESIAN_POINT('Ctrl Pts',(-16.6286838568976,-19.1743035204364,
4.32234311412888));
#161194=CARTESIAN_POINT('Ctrl Pts',(-16.6272943560971,-19.1605687008737,
4.32150028303963));
#161195=CARTESIAN_POINT('Ctrl Pts',(-16.6268523205152,-19.15605447989,4.32122414963919));
#161196=CARTESIAN_POINT('Ctrl Pts',(-16.6260915671063,-19.1480192264726,
4.3207342430941));
#161197=CARTESIAN_POINT('Ctrl Pts',(-16.6257671585498,-19.144498793391,
4.32052015434745));
#161198=CARTESIAN_POINT('Ctrl Pts',(-16.6250830412315,-19.1368656379594,
4.32005715840702));
#161199=CARTESIAN_POINT('Ctrl Pts',(-16.6247265442202,-19.1327526832205,
4.31980843322359));
#161200=CARTESIAN_POINT('Ctrl Pts',(-16.6237868683195,-19.1215300154826,
4.31913173921145));
#161201=CARTESIAN_POINT('Ctrl Pts',(-16.623227583917,-19.1144182811866,
4.31870509021443));
#161202=CARTESIAN_POINT('Ctrl Pts',(-16.6206619198955,-19.0795390470501,
4.31662263802556));
#161203=CARTESIAN_POINT('Ctrl Pts',(-16.6191673596634,-19.0517352520293,
4.31499376850785));
#161204=CARTESIAN_POINT('Ctrl Pts',(-16.6174480459763,-19.0011476052357,
4.3120736842937));
#161205=CARTESIAN_POINT('Ctrl Pts',(-16.6170417809572,-18.9783748204424,
4.31077518281084));
#161206=CARTESIAN_POINT('Ctrl Pts',(-16.6169556454356,-18.9277105634466,
4.30791337245531));
#161207=CARTESIAN_POINT('Ctrl Pts',(-16.6174593272411,-18.8998228752555,
4.30635633985962));
#161208=CARTESIAN_POINT('Ctrl Pts',(-16.6201690247286,-18.8282113321721,
4.30238731691615));
#161209=CARTESIAN_POINT('Ctrl Pts',(-16.6231804165231,-18.7845308530063,
4.29999424763356));
#161210=CARTESIAN_POINT('Ctrl Pts',(-16.6384422448624,-18.6321875904551,
4.29165862003666));
#161211=CARTESIAN_POINT('Ctrl Pts',(-16.6577514473825,-18.5244098407094,
4.28577144546639));
#161212=CARTESIAN_POINT('Ctrl Pts',(-16.7043621617311,-18.3453823325774,
4.27548482915905));
#161213=CARTESIAN_POINT('Ctrl Pts',(-16.7273378551811,-18.2732363856319,
4.27119533143887));
#161214=CARTESIAN_POINT('Ctrl Pts',(-16.7608130177595,-18.1848109353364,
4.26567516157173));
#161215=CARTESIAN_POINT('Ctrl Pts',(-16.7677379395606,-18.1672328987087,
4.2645646111783));
#161216=CARTESIAN_POINT('Ctrl Pts',(-16.7781446660458,-18.141819553038,
4.26293880282761));
#161217=CARTESIAN_POINT('Ctrl Pts',(-16.7814403886477,-18.1339086818589,
4.26242982954687));
#161218=CARTESIAN_POINT('Ctrl Pts',(-16.7873012555541,-18.120077754298,
4.26153482044794));
#161219=CARTESIAN_POINT('Ctrl Pts',(-16.7898456141496,-18.1141489708324,
4.26114949576392));
#161220=CARTESIAN_POINT('Ctrl Pts',(-16.7948375713383,-18.1026620470568,
4.26039965080252));
#161221=CARTESIAN_POINT('Ctrl Pts',(-16.7972820667713,-18.097102620803,
4.26003523965215));
#161222=CARTESIAN_POINT('Ctrl Pts',(-16.8031810063599,-18.0838420336578,
4.2591623979966));
#161223=CARTESIAN_POINT('Ctrl Pts',(-16.8066576318921,-18.0761509070661,
4.25865320912794));
#161224=CARTESIAN_POINT('Ctrl Pts',(-16.8193572420039,-18.048498124709,
4.25681170432923));
#161225=CARTESIAN_POINT('Ctrl Pts',(-16.8288448633642,-18.028660204738,
4.25547028904417));
#161226=CARTESIAN_POINT('Ctrl Pts',(-16.9218504330035,-17.8417309709721,
4.24263174756426));
#161227=CARTESIAN_POINT('Ctrl Pts',(-17.026816802389,-17.686266711004,4.23032333190481));
#161228=CARTESIAN_POINT('Ctrl Pts',(-17.2034579078826,-17.4872720984696,
4.21275803813741));
#161229=CARTESIAN_POINT('Ctrl Pts',(-17.2594402441859,-17.4309273063874,
4.20754582033244));
#161230=CARTESIAN_POINT('Ctrl Pts',(-17.3450899978938,-17.3539071244404,
4.20020448090626));
#161231=CARTESIAN_POINT('Ctrl Pts',(-17.3723276669348,-17.3306361782222,
4.19795454430411));
#161232=CARTESIAN_POINT('Ctrl Pts',(-17.40593232047,-17.3033700262208,4.19529224826232));
#161233=CARTESIAN_POINT('Ctrl Pts',(-17.4117449699798,-17.298704445285,
4.19483573493524));
#161234=CARTESIAN_POINT('Ctrl Pts',(-17.4208373847754,-17.2914849527131,
4.19412798481151));
#161235=CARTESIAN_POINT('Ctrl Pts',(-17.4241001696066,-17.2889098908023,
4.19387527310076));
#161236=CARTESIAN_POINT('Ctrl Pts',(-17.4301763850375,-17.284143381945,
4.19340702716097));
#161237=CARTESIAN_POINT('Ctrl Pts',(-17.4329877418883,-17.2819494553036,
4.1931913201905));
#161238=CARTESIAN_POINT('Ctrl Pts',(-17.4393705153862,-17.2769943654663,
4.19270370593182));
#161239=CARTESIAN_POINT('Ctrl Pts',(-17.4429452188959,-17.2742375224107,
4.1924321052258));
#161240=CARTESIAN_POINT('Ctrl Pts',(-17.4535657445287,-17.2661009218965,
4.19162948798825));
#161241=CARTESIAN_POINT('Ctrl Pts',(-17.4606366702142,-17.260753885237,
4.19110072211353));
#161242=CARTESIAN_POINT('Ctrl Pts',(-17.5135253556929,-17.2212791748119,
4.18718545958272));
#161243=CARTESIAN_POINT('Ctrl Pts',(-17.5606785595797,-17.1889710846047,
4.18391541245938));
#161244=CARTESIAN_POINT('Ctrl Pts',(-17.7373360986381,-17.078161730896,
4.17222377550504));
#161245=CARTESIAN_POINT('Ctrl Pts',(-17.8738514152183,-17.0117013736056,
4.16420804402765));
#161246=CARTESIAN_POINT('Ctrl Pts',(-18.1035139377817,-16.9289401534201,
4.15076219570785));
#161247=CARTESIAN_POINT('Ctrl Pts',(-18.1926929172031,-16.903276596604,
4.14555636384181));
#161248=CARTESIAN_POINT('Ctrl Pts',(-18.3038460490648,-16.879055120033,
4.13892983092316));
#161249=CARTESIAN_POINT('Ctrl Pts',(-18.3244970633135,-16.8748769428532,
4.13769329115882));
#161250=CARTESIAN_POINT('Ctrl Pts',(-18.354009170546,-16.8693631709015,
4.13591716638905));
#161251=CARTESIAN_POINT('Ctrl Pts',(-18.3628221173852,-16.8677744440461,
4.13538564220391));
#161252=CARTESIAN_POINT('Ctrl Pts',(-18.37806512875,-16.8651263017487,4.13446424764891));
#161253=CARTESIAN_POINT('Ctrl Pts',(-18.3844905400722,-16.8640405652931,
4.13407521953175));
#161254=CARTESIAN_POINT('Ctrl Pts',(-18.3968182073372,-16.86201599143,4.13332758941227));
#161255=CARTESIAN_POINT('Ctrl Pts',(-18.4027196348812,-16.8610724460349,
4.13296914105122));
#161256=CARTESIAN_POINT('Ctrl Pts',(-18.4181095289915,-16.8586786332849,
4.13203290742792));
#161257=CARTESIAN_POINT('Ctrl Pts',(-18.4276039248941,-16.8572678991258,
4.13145387492879));
#161258=CARTESIAN_POINT('Ctrl Pts',(-18.4601864003512,-16.8526528548455,
4.12946164038942));
#161259=CARTESIAN_POINT('Ctrl Pts',(-18.4833169877505,-16.8497654073732,
4.12803848849328));
#161260=CARTESIAN_POINT('Ctrl Pts',(-18.676284952268,-16.8289066859607,
4.11608805901549));
#161261=CARTESIAN_POINT('Ctrl Pts',(-18.8476467851267,-16.8311702138189,
4.10489891875928));
#161262=CARTESIAN_POINT('Ctrl Pts',(-19.1063780758457,-16.8660501245892,
4.08764679579089));
#161263=CARTESIAN_POINT('Ctrl Pts',(-19.1950601337237,-16.8838419152233,
4.08168373699695));
#161264=CARTESIAN_POINT('Ctrl Pts',(-19.3196747113404,-16.9172596287982,
4.07344070960928));
#161265=CARTESIAN_POINT('Ctrl Pts',(-19.3567325587045,-16.9282935386706,
4.07100783619525));
#161266=CARTESIAN_POINT('Ctrl Pts',(-19.4007095398341,-16.9427102167108,
4.06815970144026));
#161267=CARTESIAN_POINT('Ctrl Pts',(-19.4079363608653,-16.9451226172756,
4.0676929411998));
#161268=CARTESIAN_POINT('Ctrl Pts',(-19.419119611067,-16.9489229433357,
4.06697280601723));
#161269=CARTESIAN_POINT('Ctrl Pts',(-19.4230851201527,-16.9502836678763,
4.06671787331074));
#161270=CARTESIAN_POINT('Ctrl Pts',(-19.4304131787936,-16.9528225744732,
4.0662475879667));
#161271=CARTESIAN_POINT('Ctrl Pts',(-19.4337767684433,-16.9539974552095,
4.06603204949048));
#161272=CARTESIAN_POINT('Ctrl Pts',(-19.441350765548,-16.9566644774353,
4.06554742614101));
#161273=CARTESIAN_POINT('Ctrl Pts',(-19.4455594134304,-16.9581614520906,
4.06527863186256));
#161274=CARTESIAN_POINT('Ctrl Pts',(-19.4578988539727,-16.9625945163389,
4.06449191973399));
#161275=CARTESIAN_POINT('Ctrl Pts',(-19.466016550509,-16.9655671406344,
4.0639761219348));
#161276=CARTESIAN_POINT('Ctrl Pts',(-19.5224627289239,-16.986630212118,
4.0604002852531));
#161277=CARTESIAN_POINT('Ctrl Pts',(-19.5701380319181,-17.0064342721398,
4.0574350446848));
#161278=CARTESIAN_POINT('Ctrl Pts',(-19.6369264924716,-17.0370871436343,
4.05329621495599));
#161279=CARTESIAN_POINT('Ctrl Pts',(-19.6566651142311,-17.0465193175835,
4.05207499299354));
#161280=CARTESIAN_POINT('Ctrl Pts',(-19.7995539146676,-17.1175403016805,
4.04322481883443));
#161281=CARTESIAN_POINT('Ctrl Pts',(-19.9165826885246,-17.1907083248481,
4.03590143513793));
#161282=CARTESIAN_POINT('Ctrl Pts',(-20.0975672381432,-17.3300857386213,
4.02330718542647));
#161283=CARTESIAN_POINT('Ctrl Pts',(-20.1658130826768,-17.3900044663649,
4.01820667831549));
#161284=CARTESIAN_POINT('Ctrl Pts',(-20.2447378582517,-17.4688297678791,
4.0117075684252));
#161285=CARTESIAN_POINT('Ctrl Pts',(-20.2592564804963,-17.4837645158633,
4.01048494693836));
#161286=CARTESIAN_POINT('Ctrl Pts',(-20.2796703504513,-17.5053930653889,
4.0087253621927));
#161287=CARTESIAN_POINT('Ctrl Pts',(-20.2857476135237,-17.5119139623791,
4.00819625278742));
#161288=CARTESIAN_POINT('Ctrl Pts',(-20.2961911255587,-17.5232627055851,
4.00727770927457));
#161289=CARTESIAN_POINT('Ctrl Pts',(-20.3005766554149,-17.5280727018293,
4.006889103194));
#161290=CARTESIAN_POINT('Ctrl Pts',(-20.3089521336291,-17.5373443520888,
4.00614134217163));
#161291=CARTESIAN_POINT('Ctrl Pts',(-20.3129454851778,-17.5418028580787,
4.00578233634828));
#161292=CARTESIAN_POINT('Ctrl Pts',(-20.3233262532745,-17.5534921723223,
4.0048425500341));
#161293=CARTESIAN_POINT('Ctrl Pts',(-20.3296831879249,-17.5607497556598,
4.00426050367409));
#161294=CARTESIAN_POINT('Ctrl Pts',(-20.3514218806424,-17.5859133700444,
4.00224718124831));
#161295=CARTESIAN_POINT('Ctrl Pts',(-20.3665531867615,-17.6040325515282,
4.00080567044052));
#161296=CARTESIAN_POINT('Ctrl Pts',(-20.4850680651712,-17.7508728413211,
3.98918383764586));
#161297=CARTESIAN_POINT('Ctrl Pts',(-20.5733553141143,-17.8910107571822,
3.97838998571285));
#161298=CARTESIAN_POINT('Ctrl Pts',(-20.6734508076956,-18.1006783079954,
3.9630363360022));
#161299=CARTESIAN_POINT('Ctrl Pts',(-20.6995189376785,-18.1627312566259,
3.95859032807702));
#161300=CARTESIAN_POINT('Ctrl Pts',(-20.722580643286,-18.2258897982069,
3.95421663535643));
#161301=CARTESIAN_POINT('',(-20.8509992439666,-18.9537891464354,4.48828857340046));
#161302=CARTESIAN_POINT('Ctrl Pts',(-20.7225805737618,-18.2258896078024,
3.73234499902339));
#161303=CARTESIAN_POINT('Ctrl Pts',(-20.7168697221505,-18.2102494397289,
3.73327492175908));
#161304=CARTESIAN_POINT('Ctrl Pts',(-20.7109727301829,-18.1946721917005,
3.73420940116923));
#161305=CARTESIAN_POINT('Ctrl Pts',(-20.6832637474869,-18.1240088539995,
3.73849011524215));
#161306=CARTESIAN_POINT('Ctrl Pts',(-20.6593332283651,-18.0697928105943,
3.74189148108078));
#161307=CARTESIAN_POINT('Ctrl Pts',(-20.6277538838877,-18.0056728464178,
3.74609045171824));
#161308=CARTESIAN_POINT('Ctrl Pts',(-20.6222502083618,-17.9947382826347,
3.74681283467328));
#161309=CARTESIAN_POINT('Ctrl Pts',(-20.6130255220663,-17.9768000343595,
3.74800864578225));
#161310=CARTESIAN_POINT('Ctrl Pts',(-20.6093593923728,-17.969768340775,
3.74848014291643));
#161311=CARTESIAN_POINT('Ctrl Pts',(-20.6026761185634,-17.9571235391769,
3.7493330553719));
#161312=CARTESIAN_POINT('Ctrl Pts',(-20.5996729600961,-17.9515031169549,
3.74971397141702));
#161313=CARTESIAN_POINT('Ctrl Pts',(-20.5931997963148,-17.9395190601124,
3.75053009033484));
#161314=CARTESIAN_POINT('Ctrl Pts',(-20.5897224009617,-17.9331595292752,
3.75096555342475));
#161315=CARTESIAN_POINT('Ctrl Pts',(-20.5802117912778,-17.9159765604133,
3.75214866567443));
#161316=CARTESIAN_POINT('Ctrl Pts',(-20.5741161655625,-17.9051881579636,
3.7528985466986));
#161317=CARTESIAN_POINT('Ctrl Pts',(-20.5423240187755,-17.8500563176615,
3.75676760963817));
#161318=CARTESIAN_POINT('Ctrl Pts',(-20.5151198986635,-17.8066062554593,
3.75994119002768));
#161319=CARTESIAN_POINT('Ctrl Pts',(-20.3905653456497,-17.622851978179,
3.77392306328615));
#161320=CARTESIAN_POINT('Ctrl Pts',(-20.2780247687421,-17.4936399234176,
3.78529485027403));
#161321=CARTESIAN_POINT('Ctrl Pts',(-20.0828494593477,-17.3177524352721,
3.80257317049292));
#161322=CARTESIAN_POINT('Ctrl Pts',(-20.0105243814876,-17.2606545437336,
3.80854937783097));
#161323=CARTESIAN_POINT('Ctrl Pts',(-19.9267413771648,-17.2029572659246,
3.81483430344893));
#161324=CARTESIAN_POINT('Ctrl Pts',(-19.9187408255114,-17.1975280957139,
3.8154283430354));
#161325=CARTESIAN_POINT('Ctrl Pts',(-19.9068673184446,-17.1895889964345,
3.81630061898091));
#161326=CARTESIAN_POINT('Ctrl Pts',(-19.903023032076,-17.1870367019195,
3.81658160396411));
#161327=CARTESIAN_POINT('Ctrl Pts',(-19.8961854867887,-17.1825292667591,
3.81707879084146));
#161328=CARTESIAN_POINT('Ctrl Pts',(-19.8931955929792,-17.1805691209102,
3.81729532587539));
#161329=CARTESIAN_POINT('Ctrl Pts',(-19.8867759856138,-17.176383701083,
3.81775837123296));
#161330=CARTESIAN_POINT('Ctrl Pts',(-19.8833447970638,-17.1741607912693,
3.81800472415984));
#161331=CARTESIAN_POINT('Ctrl Pts',(-19.8739015151528,-17.1680816861667,
3.81867967564129));
#161332=CARTESIAN_POINT('Ctrl Pts',(-19.86787624839,-17.1642459141915,3.81910693525725));
#161333=CARTESIAN_POINT('Ctrl Pts',(-19.8354946652376,-17.1438608947054,
3.82138569286831));
#161334=CARTESIAN_POINT('Ctrl Pts',(-19.8087937604208,-17.1278629093827,
3.82320301273716));
#161335=CARTESIAN_POINT('Ctrl Pts',(-19.6393307700231,-17.0313418143417,
3.83441822222573));
#161336=CARTESIAN_POINT('Ctrl Pts',(-19.4879600044594,-16.9670293801568,
3.84307893037099));
#161337=CARTESIAN_POINT('Ctrl Pts',(-19.2182121849648,-16.8877893440932,
3.85846831213238));
#161338=CARTESIAN_POINT('Ctrl Pts',(-19.1032203073109,-16.864154665791,
3.86501037276029));
#161339=CARTESIAN_POINT('Ctrl Pts',(-18.9726798996914,-16.8484493711898,
3.87271296574712));
#161340=CARTESIAN_POINT('Ctrl Pts',(-18.9584707412171,-16.8468857005147,
3.87355476065347));
#161341=CARTESIAN_POINT('Ctrl Pts',(-18.9358327568135,-16.8446262684153,
3.87490171391459));
#161342=CARTESIAN_POINT('Ctrl Pts',(-18.9274135616089,-16.8438368902485,
3.87540392848714));
#161343=CARTESIAN_POINT('Ctrl Pts',(-18.9125575901256,-16.8425337450693,
3.87629243871259));
#161344=CARTESIAN_POINT('Ctrl Pts',(-18.9061227332175,-16.8419989438469,
3.87667806786772));
#161345=CARTESIAN_POINT('Ctrl Pts',(-18.8928091424546,-16.8409537586411,
3.87747756266242));
#161346=CARTESIAN_POINT('Ctrl Pts',(-18.8859301671272,-16.8404475380783,
3.87789155441923));
#161347=CARTESIAN_POINT('Ctrl Pts',(-18.8682679991568,-16.8392345420039,
3.87895687284404));
#161348=CARTESIAN_POINT('Ctrl Pts',(-18.8574817442179,-16.8385767039793,
3.87960972795125));
#161349=CARTESIAN_POINT('Ctrl Pts',(-18.8124547088774,-16.8361764443806,
3.88234481127979));
#161350=CARTESIAN_POINT('Ctrl Pts',(-18.7781807484749,-16.8351834502245,
3.88445034999934));
#161351=CARTESIAN_POINT('Ctrl Pts',(-18.6888394547021,-16.8347656773168,
3.89000356659341));
#161352=CARTESIAN_POINT('Ctrl Pts',(-18.6337946447766,-16.8366563589487,
3.89348960818688));
#161353=CARTESIAN_POINT('Ctrl Pts',(-18.4698251781524,-16.8487026087623,
3.90405713853167));
#161354=CARTESIAN_POINT('Ctrl Pts',(-18.3615529764208,-16.8651535753061,
3.91128702477762));
#161355=CARTESIAN_POINT('Ctrl Pts',(-18.211490921814,-16.9000076486786,
3.92146366081904));
#161356=CARTESIAN_POINT('Ctrl Pts',(-18.1682667023315,-16.911501443557,
3.92441203990845));
#161357=CARTESIAN_POINT('Ctrl Pts',(-18.101277103865,-16.9316071981858,
3.92898249715486));
#161358=CARTESIAN_POINT('Ctrl Pts',(-18.0772469763796,-16.9392901665316,
3.93062212700737));
#161359=CARTESIAN_POINT('Ctrl Pts',(-18.0061325540957,-16.9634363283126,
3.93546462661598));
#161360=CARTESIAN_POINT('Ctrl Pts',(-17.9594829648241,-16.9811370611288,
3.93862846713814));
#161361=CARTESIAN_POINT('Ctrl Pts',(-17.9062944398526,-17.0034996590645,
3.94218670786626));
#161362=CARTESIAN_POINT('Ctrl Pts',(-17.8991070586414,-17.0065684659426,
3.9426664709249));
#161363=CARTESIAN_POINT('Ctrl Pts',(-17.8876574002023,-17.0115322836678,
3.94342885061462));
#161364=CARTESIAN_POINT('Ctrl Pts',(-17.8833841857784,-17.0134016682366,
3.9437129607577));
#161365=CARTESIAN_POINT('Ctrl Pts',(-17.8758324061171,-17.0167350898375,
3.94421425445942));
#161366=CARTESIAN_POINT('Ctrl Pts',(-17.8725513443565,-17.0181933638216,
3.94443178573277));
#161367=CARTESIAN_POINT('Ctrl Pts',(-17.865611029865,-17.02129916862,3.9448913387585));
#161368=CARTESIAN_POINT('Ctrl Pts',(-17.8619527541751,-17.0229487551107,
3.94513323206303));
#161369=CARTESIAN_POINT('Ctrl Pts',(-17.8521059224498,-17.0274226152305,
3.94578346822859));
#161370=CARTESIAN_POINT('Ctrl Pts',(-17.8459261911831,-17.0302663590007,
3.94619063104797));
#161371=CARTESIAN_POINT('Ctrl Pts',(-17.8155053916162,-17.044443260245,
3.94819094726377));
#161372=CARTESIAN_POINT('Ctrl Pts',(-17.7914658130374,-17.0562060981686,
3.9497590559918));
#161373=CARTESIAN_POINT('Ctrl Pts',(-17.7228380190854,-17.0914147101625,
3.95421729099424));
#161374=CARTESIAN_POINT('Ctrl Pts',(-17.6788533313467,-17.1160009921855,
3.95705200676497));
#161375=CARTESIAN_POINT('Ctrl Pts',(-17.5228334666803,-17.2106728722606,
3.96717233163782));
#161376=CARTESIAN_POINT('Ctrl Pts',(-17.416543620544,-17.2896355191146,
3.97421052526027));
#161377=CARTESIAN_POINT('Ctrl Pts',(-17.2410259751958,-17.4474998421393,
3.98719700211521));
#161378=CARTESIAN_POINT('Ctrl Pts',(-17.1689801213214,-17.5225942139705,
3.99303628406593));
#161379=CARTESIAN_POINT('Ctrl Pts',(-17.0937843035524,-17.6135011799298,
3.99994986438718));
#161380=CARTESIAN_POINT('Ctrl Pts',(-17.0849324333799,-17.6244222174506,
4.00077789123713));
#161381=CARTESIAN_POINT('Ctrl Pts',(-17.070974088759,-17.6419984105496,
4.00210691902117));
#161382=CARTESIAN_POINT('Ctrl Pts',(-17.0657971709286,-17.6485972748951,
4.00260509890296));
#161383=CARTESIAN_POINT('Ctrl Pts',(-17.0567111757926,-17.660321731045,
4.00348892083461));
#161384=CARTESIAN_POINT('Ctrl Pts',(-17.0527860178988,-17.6654347683578,
4.00387391896328));
#161385=CARTESIAN_POINT('Ctrl Pts',(-17.0446917462228,-17.6760789217614,
4.00467453348143));
#161386=CARTESIAN_POINT('Ctrl Pts',(-17.0405263084735,-17.68161272499,4.00509028798615));
#161387=CARTESIAN_POINT('Ctrl Pts',(-17.0298536589532,-17.6959371566041,
4.00616531056579));
#161388=CARTESIAN_POINT('Ctrl Pts',(-17.0233873389283,-17.7047578683298,
4.00682616116333));
#161389=CARTESIAN_POINT('Ctrl Pts',(-16.9962585801112,-17.7423720610006,
4.0096397853944));
#161390=CARTESIAN_POINT('Ctrl Pts',(-16.9762535228617,-17.7716305336951,
4.01181757638246));
#161391=CARTESIAN_POINT('Ctrl Pts',(-16.9256652404467,-17.8497583361539,
4.01760847568817));
#161392=CARTESIAN_POINT('Ctrl Pts',(-16.8963287769265,-17.8993961651912,
4.02126416786822));
#161393=CARTESIAN_POINT('Ctrl Pts',(-16.7931670747894,-18.0914347198208,
4.03530432881969));
#161394=CARTESIAN_POINT('Ctrl Pts',(-16.7335834175254,-18.2408522016946,
4.04607042921717));
#161395=CARTESIAN_POINT('Ctrl Pts',(-16.6876803118108,-18.4093498401971,
4.05742882719627));
#161396=CARTESIAN_POINT('Ctrl Pts',(-16.6840616688482,-18.4231840446689,
4.05835545116412));
#161397=CARTESIAN_POINT('Ctrl Pts',(-16.6781716169031,-18.4466714243848,
4.05991754687039));
#161398=CARTESIAN_POINT('Ctrl Pts',(-16.6758273864821,-18.4563057307955,
4.06055515887759));
#161399=CARTESIAN_POINT('Ctrl Pts',(-16.6640323666881,-18.5063074839135,
4.06384693626785));
#161400=CARTESIAN_POINT('Ctrl Pts',(-16.6557004798112,-18.5469327822474,
4.06646291261482));
#161401=CARTESIAN_POINT('Ctrl Pts',(-16.6472919455488,-18.5950778980493,
4.0694743436486));
#161402=CARTESIAN_POINT('Ctrl Pts',(-16.6460555825447,-18.6023830600729,
4.06992887936833));
#161403=CARTESIAN_POINT('Ctrl Pts',(-16.6441148723517,-18.614227515328,
4.0706618123081));
#161404=CARTESIAN_POINT('Ctrl Pts',(-16.6433869156504,-18.6187628012485,
4.07094149668904));
#161405=CARTESIAN_POINT('Ctrl Pts',(-16.6421189503297,-18.6268301361703,
4.07143725050983));
#161406=CARTESIAN_POINT('Ctrl Pts',(-16.6415731177856,-18.6303612125954,
4.07165364588344));
#161407=CARTESIAN_POINT('Ctrl Pts',(-16.6404198651223,-18.6379489790814,
4.0721173586375));
#161408=CARTESIAN_POINT('Ctrl Pts',(-16.6398152961342,-18.6420060457917,
4.07236451355341));
#161409=CARTESIAN_POINT('Ctrl Pts',(-16.6381814540095,-18.6531931750551,
4.07304392833033));
#161410=CARTESIAN_POINT('Ctrl Pts',(-16.6371767662285,-18.6603268506334,
4.07347481963509));
#161411=CARTESIAN_POINT('Ctrl Pts',(-16.6319088623105,-18.6991656178361,
4.07580867617781));
#161412=CARTESIAN_POINT('Ctrl Pts',(-16.628328049734,-18.7309609454628,
4.07767547651267));
#161413=CARTESIAN_POINT('Ctrl Pts',(-16.6108906364366,-18.9253192593608,
4.08888643334251));
#161414=CARTESIAN_POINT('Ctrl Pts',(-16.6151425729429,-19.088968908908,
4.09750876911649));
#161415=CARTESIAN_POINT('Ctrl Pts',(-16.6546491864938,-19.3663365232059,
4.1128457270043));
#161416=CARTESIAN_POINT('Ctrl Pts',(-16.6807143096475,-19.4805708641486,
4.11937599655691));
#161417=CARTESIAN_POINT('Ctrl Pts',(-16.7203982244778,-19.6056827593115,
4.12706531716991));
#161418=CARTESIAN_POINT('Ctrl Pts',(-16.7248570590233,-19.6192614839888,
4.1279069449177));
#161419=CARTESIAN_POINT('Ctrl Pts',(-16.7321720536246,-19.6407999457756,
4.12925368066921));
#161420=CARTESIAN_POINT('Ctrl Pts',(-16.7349390562625,-19.6487896614111,
4.12975584639551));
#161421=CARTESIAN_POINT('Ctrl Pts',(-16.7399033693759,-19.6628511234073,
4.13064429971968));
#161422=CARTESIAN_POINT('Ctrl Pts',(-16.7420807467644,-19.6689298285605,
4.13102992109362));
#161423=CARTESIAN_POINT('Ctrl Pts',(-16.7466416666493,-19.6814816217122,
4.13182942873961));
#161424=CARTESIAN_POINT('Ctrl Pts',(-16.7490291032123,-19.6879532041565,
4.13224344127172));
#161425=CARTESIAN_POINT('Ctrl Pts',(-16.7552383172479,-19.7045343927794,
4.13330887419664));
#161426=CARTESIAN_POINT('Ctrl Pts',(-16.7591059275504,-19.7146265175454,
4.13396182366307));
#161427=CARTESIAN_POINT('Ctrl Pts',(-16.7755692399774,-19.7566206178897,
4.13669782121422));
#161428=CARTESIAN_POINT('Ctrl Pts',(-16.7888614373468,-19.7882422713803,
4.13880419929231));
#161429=CARTESIAN_POINT('Ctrl Pts',(-16.8254906767519,-19.8697777962227,
4.14436015730516));
#161430=CARTESIAN_POINT('Ctrl Pts',(-16.8500172953326,-19.9191257769245,
4.1478481481997));
#161431=CARTESIAN_POINT('Ctrl Pts',(-16.9289062920239,-20.0634361660146,
4.15841942326031));
#161432=CARTESIAN_POINT('Ctrl Pts',(-16.9887300524645,-20.1551969870905,
4.16565109249587));
#161433=CARTESIAN_POINT('Ctrl Pts',(-17.0840670701738,-20.2792635926364,
4.17598684778336));
#161434=CARTESIAN_POINT('Ctrl Pts',(-17.1140041876896,-20.3156425847411,
4.17909212856166));
#161435=CARTESIAN_POINT('Ctrl Pts',(-17.1581979842347,-20.3658345106149,
4.18345759856539));
#161436=CARTESIAN_POINT('Ctrl Pts',(-17.1714730647769,-20.3804920815762,
4.18474276004411));
#161437=CARTESIAN_POINT('Ctrl Pts',(-17.220851665177,-20.4335009897875,
4.18942272787567));
#161438=CARTESIAN_POINT('Ctrl Pts',(-17.2581806269553,-20.4706906354358,
4.19276953974709));
#161439=CARTESIAN_POINT('Ctrl Pts',(-17.3032424571743,-20.5123516845133,
4.19655506074864));
#161440=CARTESIAN_POINT('Ctrl Pts',(-17.3096600739558,-20.5182120886848,
4.19708843796626));
#161441=CARTESIAN_POINT('Ctrl Pts',(-17.3194380961194,-20.5270313209435,
4.1978921904044));
#161442=CARTESIAN_POINT('Ctrl Pts',(-17.3227720078672,-20.5300192004333,
4.19816468538043));
#161443=CARTESIAN_POINT('Ctrl Pts',(-17.3287766645609,-20.5353663745537,
4.198652650921));
#161444=CARTESIAN_POINT('Ctrl Pts',(-17.3314438983081,-20.5377295105773,
4.19886840743268));
#161445=CARTESIAN_POINT('Ctrl Pts',(-17.3372563150521,-20.5428531013295,
4.19933641996592));
#161446=CARTESIAN_POINT('Ctrl Pts',(-17.340403709584,-20.5456109598914,
4.19958848321721));
#161447=CARTESIAN_POINT('Ctrl Pts',(-17.3492772959581,-20.5533399180345,
4.20029538112856));
#161448=CARTESIAN_POINT('Ctrl Pts',(-17.3550221156571,-20.5582896683398,
4.2007486585063));
#161449=CARTESIAN_POINT('Ctrl Pts',(-17.3897289212988,-20.587869707223,
4.20346178695947));
#161450=CARTESIAN_POINT('Ctrl Pts',(-17.4193254743493,-20.6117486944671,
4.20567016992761));
#161451=CARTESIAN_POINT('Ctrl Pts',(-17.5193335035214,-20.6880820297534,
4.21285180062573));
#161452=CARTESIAN_POINT('Ctrl Pts',(-17.5923671122747,-20.7369572272965,
4.21765604623029));
#161453=CARTESIAN_POINT('Ctrl Pts',(-17.8188876546578,-20.8689407396943,
4.2319182372502));
#161454=CARTESIAN_POINT('Ctrl Pts',(-17.9797938389152,-20.9377640143448,
4.24129778576002));
#161455=CARTESIAN_POINT('Ctrl Pts',(-18.1694807681475,-20.9924752892524,
4.25276860950246));
#161456=CARTESIAN_POINT('Ctrl Pts',(-18.191752541717,-20.9985065359321,
4.25412028802448));
#161457=CARTESIAN_POINT('Ctrl Pts',(-18.2233847235402,-21.0065199989763,
4.25604865524583));
#161458=CARTESIAN_POINT('Ctrl Pts',(-18.2326673031133,-21.0088047815055,
4.2566155779612));
#161459=CARTESIAN_POINT('Ctrl Pts',(-18.247770759272,-21.0124139773417,
4.25753980385405));
#161460=CARTESIAN_POINT('Ctrl Pts',(-18.2535823891813,-21.0137767945768,
4.2578958661323));
#161461=CARTESIAN_POINT('Ctrl Pts',(-18.2657561712153,-21.0165772594493,
4.25864265464775));
#161462=CARTESIAN_POINT('Ctrl Pts',(-18.2721193505151,-21.0180101179771,
4.25903353051147));
#161463=CARTESIAN_POINT('Ctrl Pts',(-18.2872668470791,-21.0213475496345,
4.2599653186582));
#161464=CARTESIAN_POINT('Ctrl Pts',(-18.2960568191622,-21.0232256172517,
4.260507074363));
#161465=CARTESIAN_POINT('Ctrl Pts',(-18.3256818941194,-21.0293583044502,
4.26233663142532));
#161466=CARTESIAN_POINT('Ctrl Pts',(-18.3465685511101,-21.0333548523242,
4.26363262975263));
#161467=CARTESIAN_POINT('Ctrl Pts',(-18.5180610329841,-21.0634982453379,
4.27432675358716));
#161468=CARTESIAN_POINT('Ctrl Pts',(-18.671006367347,-21.0735725529928,
4.28424846201762));
#161469=CARTESIAN_POINT('Ctrl Pts',(-18.8986403735704,-21.0639215443319,
4.29928955277329));
#161470=CARTESIAN_POINT('Ctrl Pts',(-18.9733859392728,-21.0567598033286,
4.30426333563097));
#161471=CARTESIAN_POINT('Ctrl Pts',(-19.0689464494272,-21.042446366361,
4.31057340736452));
#161472=CARTESIAN_POINT('Ctrl Pts',(-19.0902487570828,-21.038921656892,
4.31197670313412));
#161473=CARTESIAN_POINT('Ctrl Pts',(-19.1624906348318,-21.0258299955245,
4.31671694991476));
#161474=CARTESIAN_POINT('Ctrl Pts',(-19.2131355584661,-21.0147179039281,
4.32000857355429));
#161475=CARTESIAN_POINT('Ctrl Pts',(-19.2717049571741,-20.9995930439963,
4.3237396361131));
#161476=CARTESIAN_POINT('Ctrl Pts',(-19.2800710662406,-20.9973777869312,
4.32427075368187));
#161477=CARTESIAN_POINT('Ctrl Pts',(-19.2927365011485,-20.9939408644478,
4.32507178270113));
#161478=CARTESIAN_POINT('Ctrl Pts',(-19.2970458135304,-20.9927568165587,
4.32534379289797));
#161479=CARTESIAN_POINT('Ctrl Pts',(-19.3047840644833,-20.9906042398618,
4.32583124232455));
#161480=CARTESIAN_POINT('Ctrl Pts',(-19.3082143191658,-20.9896406972988,
4.32604696479259));
#161481=CARTESIAN_POINT('Ctrl Pts',(-19.3156739781137,-20.9875249804295,
4.32651530853815));
#161482=CARTESIAN_POINT('Ctrl Pts',(-19.3197023857499,-20.9863695039969,
4.32676773484543));
#161483=CARTESIAN_POINT('Ctrl Pts',(-19.3310372398869,-20.9830818456228,
4.3274766784815));
#161484=CARTESIAN_POINT('Ctrl Pts',(-19.3383357426789,-20.9809221876494,
4.32793162403818));
#161485=CARTESIAN_POINT('Ctrl Pts',(-19.3825006867438,-20.9675941334572,
4.33067612958164));
#161486=CARTESIAN_POINT('Ctrl Pts',(-19.4190708346027,-20.9554598132532,
4.3329128273252));
#161487=CARTESIAN_POINT('Ctrl Pts',(-19.5397207533015,-20.9117365783304,
4.34023440044692));
#161488=CARTESIAN_POINT('Ctrl Pts',(-19.6221241974076,-20.8757960807179,
4.34514267545348));
#161489=CARTESIAN_POINT('Ctrl Pts',(-19.8194143922129,-20.7743596654897,
4.35720611269695));
#161490=CARTESIAN_POINT('Ctrl Pts',(-19.9309150909577,-20.7031455672504,
4.36432152674259));
#161491=CARTESIAN_POINT('Ctrl Pts',(-20.0786549033234,-20.5880461256331,
4.37491345477961));
#161492=CARTESIAN_POINT('Ctrl Pts',(-20.1209047998701,-20.5523868420532,
4.37809311767221));
#161493=CARTESIAN_POINT('Ctrl Pts',(-20.1705533815596,-20.5070391854187,
4.38204488634361));
#161494=CARTESIAN_POINT('Ctrl Pts',(-20.1793290715956,-20.4988860178472,
4.3827519558898));
#161495=CARTESIAN_POINT('Ctrl Pts',(-20.1937395371283,-20.4852681066787,
4.38392758240623));
#161496=CARTESIAN_POINT('Ctrl Pts',(-20.1994140270802,-20.4798456498979,
4.38439432077853));
#161497=CARTESIAN_POINT('Ctrl Pts',(-20.2096363750362,-20.4699679900609,
4.38524212799756));
#161498=CARTESIAN_POINT('Ctrl Pts',(-20.2141945581368,-20.4655235706366,
4.38562272430894));
#161499=CARTESIAN_POINT('Ctrl Pts',(-20.2230070130457,-20.4568531729851,
4.38636356221871));
#161500=CARTESIAN_POINT('Ctrl Pts',(-20.2272635173306,-20.4526295424922,
4.38672369852369));
#161501=CARTESIAN_POINT('Ctrl Pts',(-20.2390028832041,-20.4408814366082,
4.38772339568961));
#161502=CARTESIAN_POINT('Ctrl Pts',(-20.2464471236839,-20.4333187713544,
4.3883646522824));
#161503=CARTESIAN_POINT('Ctrl Pts',(-20.277859433537,-20.4009231134952,
4.39110220598966));
#161504=CARTESIAN_POINT('Ctrl Pts',(-20.3012740847431,-20.3755630869155,
4.39322224941792));
#161505=CARTESIAN_POINT('Ctrl Pts',(-20.3609390066158,-20.3076840678458,
4.3988413133372));
#161506=CARTESIAN_POINT('Ctrl Pts',(-20.3961425504659,-20.2642846916682,
4.40238019096822));
#161507=CARTESIAN_POINT('Ctrl Pts',(-20.4700011956537,-20.1654846202707,
4.41031397141715));
#161508=CARTESIAN_POINT('Ctrl Pts',(-20.5078047722082,-20.1095235261941,
4.41472963716753));
#161509=CARTESIAN_POINT('Ctrl Pts',(-20.6208277875352,-19.9236411078564,
4.42906585649656));
#161510=CARTESIAN_POINT('Ctrl Pts',(-20.6849387302686,-19.7874937439154,
4.43910103211185));
#161511=CARTESIAN_POINT('Ctrl Pts',(-20.7392626760684,-19.6308647095153,
4.44944310789046));
#161512=CARTESIAN_POINT('Ctrl Pts',(-20.7442442921562,-19.6159680813706,
4.45041491264633));
#161513=CARTESIAN_POINT('Ctrl Pts',(-20.7508357270801,-19.5955030738574,
4.45173255597078));
#161514=CARTESIAN_POINT('Ctrl Pts',(-20.7525890218951,-19.5899819108629,
4.45208631193859));
#161515=CARTESIAN_POINT('Ctrl Pts',(-20.7553388603962,-19.5811977830754,
4.45264631902943));
#161516=CARTESIAN_POINT('Ctrl Pts',(-20.7563502019316,-19.5779395337446,
4.45285342558835));
#161517=CARTESIAN_POINT('Ctrl Pts',(-20.7584224470292,-19.5712059103387,
4.4532801523043));
#161518=CARTESIAN_POINT('Ctrl Pts',(-20.7594822797561,-19.5677302477369,
4.45349970374035));
#161519=CARTESIAN_POINT('Ctrl Pts',(-20.7619859826601,-19.5594430748376,
4.45402153234239));
#161520=CARTESIAN_POINT('Ctrl Pts',(-20.763421696862,-19.5546290837025,
4.45432333355589));
#161521=CARTESIAN_POINT('Ctrl Pts',(-20.7682044078215,-19.5383815760942,
4.45533760250583));
#161522=CARTESIAN_POINT('Ctrl Pts',(-20.7714720955077,-19.5269246909914,
4.45604559944944));
#161523=CARTESIAN_POINT('Ctrl Pts',(-20.8080701392433,-19.3943755823844,
4.46416013233734));
#161524=CARTESIAN_POINT('Ctrl Pts',(-20.8306623676895,-19.2705577245453,
4.47101316477815));
#161525=CARTESIAN_POINT('Ctrl Pts',(-20.8479900579051,-19.0817297789905,
4.48131925557765));
#161526=CARTESIAN_POINT('Ctrl Pts',(-20.8509451663437,-19.0177762435095,
4.48478351540402));
#161527=CARTESIAN_POINT('Ctrl Pts',(-20.8509992439666,-18.9537891464354,
4.48828857340046));
#161528=CARTESIAN_POINT('Ctrl Pts',(-20.850999245597,-18.9537872161824,
4.48828867913505));
#161529=CARTESIAN_POINT('Ctrl Pts',(-20.8510695256919,-18.8705388048596,
4.49284882620142));
#161530=CARTESIAN_POINT('Ctrl Pts',(-20.8462293926872,-18.7873633754263,
4.49747288514878));
#161531=CARTESIAN_POINT('Ctrl Pts',(-20.8325134503724,-18.6707567027903,
4.50419748944219));
#161532=CARTESIAN_POINT('Ctrl Pts',(-20.8277010638379,-18.636925153178,
4.50617704217313));
#161533=CARTESIAN_POINT('Ctrl Pts',(-20.8203844097302,-18.5931211120813,
4.50878341840881));
#161534=CARTESIAN_POINT('Ctrl Pts',(-20.8186232354125,-18.5830285617623,
4.50938693124433));
#161535=CARTESIAN_POINT('Ctrl Pts',(-20.8155220318927,-18.5659882221832,
4.51041115234559));
#161536=CARTESIAN_POINT('Ctrl Pts',(-20.8142202897792,-18.5590335815711,
4.51083064729524));
#161537=CARTESIAN_POINT('Ctrl Pts',(-20.8115755323949,-18.5452852796706,
4.51166292069851));
#161538=CARTESIAN_POINT('Ctrl Pts',(-20.8102339970038,-18.5384914215251,
4.51207564743034));
#161539=CARTESIAN_POINT('Ctrl Pts',(-20.8075793318785,-18.5253862276186,
4.51287464056693));
#161540=CARTESIAN_POINT('Ctrl Pts',(-20.8062706592279,-18.5190740596167,
4.51326076035452));
#161541=CARTESIAN_POINT('Ctrl Pts',(-20.8031923985453,-18.5045603800297,
4.51415156749671));
#161542=CARTESIAN_POINT('Ctrl Pts',(-20.8014028510898,-18.4963632544922,
4.51465688989135));
#161543=CARTESIAN_POINT('Ctrl Pts',(-20.7964824170247,-18.4744508519889,
4.51601371912014));
#161544=CARTESIAN_POINT('Ctrl Pts',(-20.7932635065878,-18.4607559621306,
4.51686803926679));
#161545=CARTESIAN_POINT('Ctrl Pts',(-20.7715055583977,-18.3721604885119,
4.52243681453723));
#161546=CARTESIAN_POINT('Ctrl Pts',(-20.7490266170535,-18.2983167241065,
4.52727678947559));
#161547=CARTESIAN_POINT('Ctrl Pts',(-20.7225805465488,-18.2258895332749,
4.53222344315201));
#161548=CARTESIAN_POINT('Origin',(-18.734,-18.952,0.));
#161549=CARTESIAN_POINT('',(-20.7225805962997,-18.2258896695266,5.55626859415409));
#161550=CARTESIAN_POINT('',(-20.7225805585332,-18.2258895660964,5.33540095489714));
#161551=CARTESIAN_POINT('',(-20.7225805737622,-18.2258896078036,0.));
#161552=CARTESIAN_POINT('Ctrl Pts',(-20.7225805962997,-18.2258896695266,
5.55626859415409));
#161553=CARTESIAN_POINT('Ctrl Pts',(-20.7320990939749,-18.2519577462201,
5.55474542935323));
#161554=CARTESIAN_POINT('Ctrl Pts',(-20.7411068523736,-18.2782180382529,
5.55321409559504));
#161555=CARTESIAN_POINT('Ctrl Pts',(-20.7754133681831,-18.385036223238,
5.54697995143813));
#161556=CARTESIAN_POINT('Ctrl Pts',(-20.7963949754118,-18.4668804316982,
5.54218754382626));
#161557=CARTESIAN_POINT('Ctrl Pts',(-20.8151326641375,-18.5636990555802,
5.53639859959952));
#161558=CARTESIAN_POINT('Ctrl Pts',(-20.817691286621,-18.5776720735792,
5.53556038790442));
#161559=CARTESIAN_POINT('Ctrl Pts',(-20.8214097414357,-18.599199818088,
5.5342643715788));
#161560=CARTESIAN_POINT('Ctrl Pts',(-20.8226696399543,-18.6067370135883,
5.53380975054751));
#161561=CARTESIAN_POINT('Ctrl Pts',(-20.8248931361726,-18.6204965495217,
5.53297817438786));
#161562=CARTESIAN_POINT('Ctrl Pts',(-20.8258698386648,-18.6267167060361,
5.53260164016139));
#161563=CARTESIAN_POINT('Ctrl Pts',(-20.8279419770428,-18.6403085844017,
5.53177749068674));
#161564=CARTESIAN_POINT('Ctrl Pts',(-20.8290262605791,-18.6476818982542,
5.53132952710003));
#161565=CARTESIAN_POINT('Ctrl Pts',(-20.8318905539539,-18.6679007246484,
5.53009865754964));
#161566=CARTESIAN_POINT('Ctrl Pts',(-20.8335914771489,-18.680756950372,
5.52931326311956));
#161567=CARTESIAN_POINT('Ctrl Pts',(-20.8416314800243,-18.7461410913131,
5.52530442004773));
#161568=CARTESIAN_POINT('Ctrl Pts',(-20.8461174153946,-18.7988739479112,
5.52202314179027));
#161569=CARTESIAN_POINT('Ctrl Pts',(-20.8502336388908,-18.8856700870332,
5.51653987840504));
#161570=CARTESIAN_POINT('Ctrl Pts',(-20.8510257893312,-18.9196565836178,
5.51437232070036));
#161571=CARTESIAN_POINT('Ctrl Pts',(-20.8508977918913,-19.0842687682467,
5.50378110567431));
#161572=CARTESIAN_POINT('Ctrl Pts',(-20.8387067138667,-19.2145945166531,
5.49508956453502));
#161573=CARTESIAN_POINT('Ctrl Pts',(-20.7970384706232,-19.4363469421699,
5.48023965567002));
#161574=CARTESIAN_POINT('Ctrl Pts',(-20.7732180764462,-19.5284664748066,
5.4740598682392));
#161575=CARTESIAN_POINT('Ctrl Pts',(-20.7402342465002,-19.627874953247,
5.46758880239061));
#161576=CARTESIAN_POINT('Ctrl Pts',(-20.7371210646396,-19.6370465771283,
5.46699371560475));
#161577=CARTESIAN_POINT('Ctrl Pts',(-20.7324307946542,-19.65055900348,5.46612020156299));
#161578=CARTESIAN_POINT('Ctrl Pts',(-20.73090232296,-19.6549163789916,5.46583901464156));
#161579=CARTESIAN_POINT('Ctrl Pts',(-20.7281650633119,-19.6626387860193,
5.46534160466696));
#161580=CARTESIAN_POINT('Ctrl Pts',(-20.7269619965802,-19.6660057876478,
5.4651250473556));
#161581=CARTESIAN_POINT('Ctrl Pts',(-20.7243657194792,-19.6732142537527,
5.46466210288583));
#161582=CARTESIAN_POINT('Ctrl Pts',(-20.7229699196435,-19.6770547265529,
5.46441587234752));
#161583=CARTESIAN_POINT('Ctrl Pts',(-20.7191070461289,-19.6875881295587,
5.46374160139872));
#161584=CARTESIAN_POINT('Ctrl Pts',(-20.7166172253563,-19.6942727409491,
5.46331489543619));
#161585=CARTESIAN_POINT('Ctrl Pts',(-20.7031297619653,-19.7299314999597,
5.46104439826444));
#161586=CARTESIAN_POINT('Ctrl Pts',(-20.6915300523097,-19.7586757470262,
5.45923449245834));
#161587=CARTESIAN_POINT('Ctrl Pts',(-20.6147736122224,-19.9374619914397,
5.44804390875201));
#161588=CARTESIAN_POINT('Ctrl Pts',(-20.5330352574374,-20.0797983909561,
5.43939877325784));
#161589=CARTESIAN_POINT('Ctrl Pts',(-20.3657124170988,-20.3059019476789,
5.42400426268554));
#161590=CARTESIAN_POINT('Ctrl Pts',(-20.2879589804636,-20.3944777437368,
5.4174378463749));
#161591=CARTESIAN_POINT('Ctrl Pts',(-20.1929613257168,-20.4860551997828,
5.40970784017757));
#161592=CARTESIAN_POINT('Ctrl Pts',(-20.1825655589441,-20.4958754199795,
5.40886571333382));
#161593=CARTESIAN_POINT('Ctrl Pts',(-20.1658644144752,-20.5113347404798,
5.40751832816367));
#161594=CARTESIAN_POINT('Ctrl Pts',(-20.1596232407252,-20.517042781091,
5.40701601660862));
#161595=CARTESIAN_POINT('Ctrl Pts',(-20.1485570617929,-20.5270425442269,
5.40612739340277));
#161596=CARTESIAN_POINT('Ctrl Pts',(-20.1437462841084,-20.5313499011332,
5.40574174879371));
#161597=CARTESIAN_POINT('Ctrl Pts',(-20.1337566254966,-20.5402121889069,
5.40494227948084));
#161598=CARTESIAN_POINT('Ctrl Pts',(-20.1285750471709,-20.5447639510207,
5.40452832894341));
#161599=CARTESIAN_POINT('Ctrl Pts',(-20.1152202524201,-20.5563803552348,
5.40346323768274));
#161600=CARTESIAN_POINT('Ctrl Pts',(-20.1070151075129,-20.5634078371799,
5.40281056977836));
#161601=CARTESIAN_POINT('Ctrl Pts',(-20.072567336689,-20.5924572900762,
5.40007729926763));
#161602=CARTESIAN_POINT('Ctrl Pts',(-20.045847087181,-20.6139024158623,
5.39797342479381));
#161603=CARTESIAN_POINT('Ctrl Pts',(-19.9749016419944,-20.6680644784892,
5.3924256423955));
#161604=CARTESIAN_POINT('Ctrl Pts',(-19.9299030056876,-20.6997211916748,
5.38894346429663));
#161605=CARTESIAN_POINT('Ctrl Pts',(-19.8068133684807,-20.7793343126961,
5.37952170024796));
#161606=CARTESIAN_POINT('Ctrl Pts',(-19.7267586041929,-20.8240329402428,
5.37349494489065));
#161607=CARTESIAN_POINT('Ctrl Pts',(-19.5956096943228,-20.8864762017771,
5.36389726998934));
#161608=CARTESIAN_POINT('Ctrl Pts',(-19.5462916510206,-20.9076972876215,
5.3603473547928));
#161609=CARTESIAN_POINT('Ctrl Pts',(-19.46184805834,-20.9402865963154,5.3544124441374));
#161610=CARTESIAN_POINT('Ctrl Pts',(-19.4271344415691,-20.9526527033317,
5.35201230835054));
#161611=CARTESIAN_POINT('Ctrl Pts',(-19.3471261965966,-20.9788215852332,
5.34659427775521));
#161612=CARTESIAN_POINT('Ctrl Pts',(-19.3016530781386,-20.9920245603641,
5.3435963624006));
#161613=CARTESIAN_POINT('Ctrl Pts',(-19.2483054253403,-21.0055915572527,
5.3402024991186));
#161614=CARTESIAN_POINT('Ctrl Pts',(-19.2408284606263,-21.0074496515824,
5.33972961739137));
#161615=CARTESIAN_POINT('Ctrl Pts',(-19.2288403586848,-21.0103594127946,
5.33897606882577));
#161616=CARTESIAN_POINT('Ctrl Pts',(-19.2243357048836,-21.0114371440469,
5.3386939612166));
#161617=CARTESIAN_POINT('Ctrl Pts',(-19.2163370376984,-21.0133230806223,
5.33819493760871));
#161618=CARTESIAN_POINT('Ctrl Pts',(-19.2128444657841,-21.014137201778,
5.33797768473212));
#161619=CARTESIAN_POINT('Ctrl Pts',(-19.2054215107038,-21.015847622707,
5.33751732307798));
#161620=CARTESIAN_POINT('Ctrl Pts',(-19.2014906401088,-21.0167415704012,
5.33727434989112));
#161621=CARTESIAN_POINT('Ctrl Pts',(-19.1908396926436,-21.0191318034293,
5.33661814244093));
#161622=CARTESIAN_POINT('Ctrl Pts',(-19.1841147638346,-21.0206065599516,
5.33620612582413));
#161623=CARTESIAN_POINT('Ctrl Pts',(-19.1502495377332,-21.0278601358075,
5.33414235463855));
#161624=CARTESIAN_POINT('Ctrl Pts',(-19.1230032941099,-21.0331380505443,
5.33251759368829));
#161625=CARTESIAN_POINT('Ctrl Pts',(-19.0432774335999,-21.0469613027593,
5.32784622894791));
#161626=CARTESIAN_POINT('Ctrl Pts',(-18.9905679072737,-21.0540678087979,
5.32486157307193));
#161627=CARTESIAN_POINT('Ctrl Pts',(-18.7975190746788,-21.0727245317466,
5.31413089258638));
#161628=CARTESIAN_POINT('Ctrl Pts',(-18.6563924159986,-21.0722562367394,
5.30664728833413));
#161629=CARTESIAN_POINT('Ctrl Pts',(-18.4249583140915,-21.0483359736485,
5.29377739315979));
#161630=CARTESIAN_POINT('Ctrl Pts',(-18.3342855036138,-21.0329508897311,
5.28858530666603));
#161631=CARTESIAN_POINT('Ctrl Pts',(-18.231513554845,-21.0085470628715,
5.28239285691151));
#161632=CARTESIAN_POINT('Ctrl Pts',(-18.218153439244,-21.005236655084,5.28158189924194));
#161633=CARTESIAN_POINT('Ctrl Pts',(-18.1967890293315,-20.9997212418233,
5.28027512348966));
#161634=CARTESIAN_POINT('Ctrl Pts',(-18.1887636370328,-20.9975989872708,
5.27978197769535));
#161635=CARTESIAN_POINT('Ctrl Pts',(-18.1745419070837,-20.9937485206113,
5.27890396997101));
#161636=CARTESIAN_POINT('Ctrl Pts',(-18.168340541722,-20.9920391552611,
5.2785197239155));
#161637=CARTESIAN_POINT('Ctrl Pts',(-18.1554415226266,-20.9884202887534,
5.27771753767462));
#161638=CARTESIAN_POINT('Ctrl Pts',(-18.1487453172299,-20.9865059495316,
5.27729944381542));
#161639=CARTESIAN_POINT('Ctrl Pts',(-18.1313918791334,-20.9814521144882,
5.2762115710938));
#161640=CARTESIAN_POINT('Ctrl Pts',(-18.1207497996914,-20.9782617345215,
5.27554013706721));
#161641=CARTESIAN_POINT('Ctrl Pts',(-18.0747523316687,-20.9640766363893,
5.27261908344881));
#161642=CARTESIAN_POINT('Ctrl Pts',(-18.0396654119785,-20.952239757448,
5.27034200643461));
#161643=CARTESIAN_POINT('Ctrl Pts',(-17.9473895480668,-20.9183892430523,
5.26421874866686));
#161644=CARTESIAN_POINT('Ctrl Pts',(-17.8908183251948,-20.8948037004754,
5.26032365529616));
#161645=CARTESIAN_POINT('Ctrl Pts',(-17.6944466185338,-20.8027394395837,
5.2463168607768));
#161646=CARTESIAN_POINT('Ctrl Pts',(-17.5612676906098,-20.7213503680756,
5.23587293866638));
#161647=CARTESIAN_POINT('Ctrl Pts',(-17.4256023732808,-20.6163434452836,
5.22471978443441));
#161648=CARTESIAN_POINT('Ctrl Pts',(-17.4130984808814,-20.6064372608426,
5.22368701034349));
#161649=CARTESIAN_POINT('Ctrl Pts',(-17.3725517901845,-20.5735614945797,
5.22032500008119));
#161650=CARTESIAN_POINT('Ctrl Pts',(-17.3449852768872,-20.5500116787952,
5.21801848939177));
#161651=CARTESIAN_POINT('Ctrl Pts',(-17.305541829119,-20.5145231864353,
5.21470356088933));
#161652=CARTESIAN_POINT('Ctrl Pts',(-17.2931819286684,-20.5031333856305,
5.21366261490008));
#161653=CARTESIAN_POINT('Ctrl Pts',(-17.2766273317193,-20.4875094837152,
5.21226699678137));
#161654=CARTESIAN_POINT('Ctrl Pts',(-17.2723133256403,-20.4834034533058,
5.21190317838199));
#161655=CARTESIAN_POINT('Ctrl Pts',(-17.2655322335265,-20.476894513707,
5.21133117764928));
#161656=CARTESIAN_POINT('Ctrl Pts',(-17.2630536237669,-20.474503733245,
5.21112207515763));
#161657=CARTESIAN_POINT('Ctrl Pts',(-17.2579847596926,-20.4695905514969,
5.21069441932304));
#161658=CARTESIAN_POINT('Ctrl Pts',(-17.2553951358538,-20.4670675653159,
5.2104759211946));
#161659=CARTESIAN_POINT('Ctrl Pts',(-17.2493007956321,-20.4610995406159,
5.20996165229366));
#161660=CARTESIAN_POINT('Ctrl Pts',(-17.2458015641383,-20.4576488858785,
5.20966632019869));
#161661=CARTESIAN_POINT('Ctrl Pts',(-17.2343063843572,-20.4462340581502,
5.20869583950129));
#161662=CARTESIAN_POINT('Ctrl Pts',(-17.2263619453711,-20.4382179753091,
5.20802465250578));
#161663=CARTESIAN_POINT('Ctrl Pts',(-17.2076029501314,-20.4189845964016,
5.20643751193313));
#161664=CARTESIAN_POINT('Ctrl Pts',(-17.1968472436489,-20.4077105457049,
5.20552566059723));
#161665=CARTESIAN_POINT('Ctrl Pts',(-17.1579279519793,-20.3660032398131,
5.2022147269221));
#161666=CARTESIAN_POINT('Ctrl Pts',(-17.1305342343258,-20.3348616038547,
5.19986187949899));
#161667=CARTESIAN_POINT('Ctrl Pts',(-17.0382569739199,-20.2235272329372,
5.1917747795191));
#161668=CARTESIAN_POINT('Ctrl Pts',(-16.9783299183852,-20.1394134549622,
5.18622093521156));
#161669=CARTESIAN_POINT('Ctrl Pts',(-16.8492616557765,-19.9269855375339,
5.17270455541167));
#161670=CARTESIAN_POINT('Ctrl Pts',(-16.7867686653616,-19.7952779304493,
5.16470175202433));
#161671=CARTESIAN_POINT('Ctrl Pts',(-16.7335073509736,-19.6447638562186,
5.15534808615831));
#161672=CARTESIAN_POINT('Ctrl Pts',(-16.7288835867194,-19.6312648626565,
5.15450780240407));
#161673=CARTESIAN_POINT('Ctrl Pts',(-16.7217399386323,-19.6097004061198,
5.15316281559621));
#161674=CARTESIAN_POINT('Ctrl Pts',(-16.7191312221228,-19.6016646700917,
5.15266104273462));
#161675=CARTESIAN_POINT('Ctrl Pts',(-16.7146140928229,-19.5874614351978,
5.15177304694336));
#161676=CARTESIAN_POINT('Ctrl Pts',(-16.7126856497075,-19.5813003842409,
5.15138748803535));
#161677=CARTESIAN_POINT('Ctrl Pts',(-16.7087542489773,-19.5685356982459,
5.15058787643289));
#161678=CARTESIAN_POINT('Ctrl Pts',(-16.706755340773,-19.5619309052087,
5.15017369632704));
#161679=CARTESIAN_POINT('Ctrl Pts',(-16.7017051435544,-19.5449449342119,
5.14910733993762));
#161680=CARTESIAN_POINT('Ctrl Pts',(-16.6987011153821,-19.5345500167439,
5.14845362946145));
#161681=CARTESIAN_POINT('Ctrl Pts',(-16.6864782806407,-19.4910061595938,
5.14571024768578));
#161682=CARTESIAN_POINT('Ctrl Pts',(-16.6779890411347,-19.4576595199721,
5.1435970886076));
#161683=CARTESIAN_POINT('Ctrl Pts',(-16.6579770921975,-19.3701857256668,
5.138018966348));
#161684=CARTESIAN_POINT('Ctrl Pts',(-16.6477578552025,-19.3157901837531,
5.13451520904312));
#161685=CARTESIAN_POINT('Ctrl Pts',(-16.6236834456273,-19.1526521921083,
5.12391366090748));
#161686=CARTESIAN_POINT('Ctrl Pts',(-16.6161281154048,-19.0431728121681,
5.11666758811027));
#161687=CARTESIAN_POINT('Ctrl Pts',(-16.6176040924039,-18.8732644851859,
5.10544395485926));
#161688=CARTESIAN_POINT('Ctrl Pts',(-16.6207084800713,-18.8129661559535,
5.10146795922218));
#161689=CARTESIAN_POINT('Ctrl Pts',(-16.631866298205,-18.6948640367435,
5.09377757539713));
#161690=CARTESIAN_POINT('Ctrl Pts',(-16.639741305982,-18.6370923399227,
5.09006219147965));
#161691=CARTESIAN_POINT('Ctrl Pts',(-16.6515574770134,-18.5709469105798,
5.08591579450477));
#161692=CARTESIAN_POINT('Ctrl Pts',(-16.6531790026899,-18.5621894023436,
5.08536902531434));
#161693=CARTESIAN_POINT('Ctrl Pts',(-16.6557073108253,-18.5490000545843,
5.08454915366039));
#161694=CARTESIAN_POINT('Ctrl Pts',(-16.656573085641,-18.544560588238,5.08427380500038));
#161695=CARTESIAN_POINT('Ctrl Pts',(-16.6581470321114,-18.5366252563615,
5.08378277694119));
#161696=CARTESIAN_POINT('Ctrl Pts',(-16.6588498142237,-18.5331283859793,
5.08356679568525));
#161697=CARTESIAN_POINT('Ctrl Pts',(-16.6603894328382,-18.5255666069461,
5.0831006217891));
#161698=CARTESIAN_POINT('Ctrl Pts',(-16.6612293827033,-18.5215023905906,
5.0828506093918));
#161699=CARTESIAN_POINT('Ctrl Pts',(-16.6636051997308,-18.5101748250063,
5.08215523248421));
#161700=CARTESIAN_POINT('Ctrl Pts',(-16.6651673473983,-18.5029169637195,
5.08171134480171));
#161701=CARTESIAN_POINT('Ctrl Pts',(-16.6743850952166,-18.4611596486151,
5.07916626318092));
#161702=CARTESIAN_POINT('Ctrl Pts',(-16.6828658790819,-18.4268457799038,
5.07710940487219));
#161703=CARTESIAN_POINT('Ctrl Pts',(-16.7127046556053,-18.3179041069915,
5.07064362912736));
#161704=CARTESIAN_POINT('Ctrl Pts',(-16.7373094376311,-18.2442280455371,
5.06636752551238));
#161705=CARTESIAN_POINT('Ctrl Pts',(-16.8357150806297,-17.9959106470385,
5.05179380847907));
#161706=CARTESIAN_POINT('Ctrl Pts',(-16.9288462779434,-17.8299452343977,
5.04167931543869));
#161707=CARTESIAN_POINT('Ctrl Pts',(-17.055864877666,-17.6612551605165,
5.02939282215334));
#161708=CARTESIAN_POINT('Ctrl Pts',(-17.0691808837866,-17.6441250104138,
5.02812061338992));
#161709=CARTESIAN_POINT('Ctrl Pts',(-17.0880100217009,-17.6206561519008,
5.02634178905651));
#161710=CARTESIAN_POINT('Ctrl Pts',(-17.09330140717,-17.6141406744599,5.02584403293302));
#161711=CARTESIAN_POINT('Ctrl Pts',(-17.1024800924234,-17.6029749725938,
5.02498415881919));
#161712=CARTESIAN_POINT('Ctrl Pts',(-17.106348899909,-17.5983096260279,
5.02462279199697));
#161713=CARTESIAN_POINT('Ctrl Pts',(-17.1143816338957,-17.5887072727857,
5.02387465494208));
#161714=CARTESIAN_POINT('Ctrl Pts',(-17.1185482215765,-17.5837725839421,
5.02348777801813));
#161715=CARTESIAN_POINT('Ctrl Pts',(-17.1283239173964,-17.5723016628018,
5.02258278396236));
#161716=CARTESIAN_POINT('Ctrl Pts',(-17.1339504336124,-17.5657804771283,
5.02206395131675));
#161717=CARTESIAN_POINT('Ctrl Pts',(-17.1522004083113,-17.5448877290204,
5.02038750539962));
#161718=CARTESIAN_POINT('Ctrl Pts',(-17.1649786280055,-17.5306531781655,
5.0192234514144));
#161719=CARTESIAN_POINT('Ctrl Pts',(-17.230447603557,-17.4596815094645,
5.01330633636717));
#161720=CARTESIAN_POINT('Ctrl Pts',(-17.2860244426002,-17.405698372404,
5.00843008756804));
#161721=CARTESIAN_POINT('Ctrl Pts',(-17.4460897109082,-17.2664333449365,
4.99477785312247));
#161722=CARTESIAN_POINT('Ctrl Pts',(-17.5559601144885,-17.1878955537262,
4.98580051803567));
#161723=CARTESIAN_POINT('Ctrl Pts',(-17.7149109337702,-17.0957819939485,
4.97372323715053));
#161724=CARTESIAN_POINT('Ctrl Pts',(-17.7581287537793,-17.0727013045635,
4.97052590718076));
#161725=CARTESIAN_POINT('Ctrl Pts',(-17.8414844967424,-17.0318364595991,
4.96456640732377));
#161726=CARTESIAN_POINT('Ctrl Pts',(-17.8814523113951,-17.0137598198785,
4.96179517689643));
#161727=CARTESIAN_POINT('Ctrl Pts',(-17.9289120917072,-16.9940471921087,
4.95862781609513));
#161728=CARTESIAN_POINT('Ctrl Pts',(-17.9358838622746,-16.9911949682367,
4.95816560378432));
#161729=CARTESIAN_POINT('Ctrl Pts',(-17.947165780133,-16.9866495601573,
4.95742275633351));
#161730=CARTESIAN_POINT('Ctrl Pts',(-17.9514664473751,-16.9849332291708,
4.95714077791609));
#161731=CARTESIAN_POINT('Ctrl Pts',(-17.9590991312861,-16.9819161344486,
4.95664249199223));
#161732=CARTESIAN_POINT('Ctrl Pts',(-17.9624288455908,-16.9806096916112,
4.95642584584564));
#161733=CARTESIAN_POINT('Ctrl Pts',(-17.9695621264708,-16.9778317272273,
4.9559632898184));
#161734=CARTESIAN_POINT('Ctrl Pts',(-17.9733666282959,-16.9763627594611,
4.95571753353962));
#161735=CARTESIAN_POINT('Ctrl Pts',(-17.9838031937001,-16.9723676814884,
4.95504589833326));
#161736=CARTESIAN_POINT('Ctrl Pts',(-17.9904438219302,-16.9698638851024,
4.9546213365227));
#161737=CARTESIAN_POINT('Ctrl Pts',(-18.0256827101666,-16.9567793559822,
4.95238249163214));
#161738=CARTESIAN_POINT('Ctrl Pts',(-18.0544960802675,-16.9467834424431,
4.95060098467386));
#161739=CARTESIAN_POINT('Ctrl Pts',(-18.2377752046706,-16.8876050835041,
4.93951745963536));
#161740=CARTESIAN_POINT('Ctrl Pts',(-18.3972603588826,-16.8556736823997,
4.93094268497014));
#161741=CARTESIAN_POINT('Ctrl Pts',(-18.6781020273253,-16.8323572495901,
4.91552930121469));
#161742=CARTESIAN_POINT('Ctrl Pts',(-18.7979705985112,-16.8325868265202,
4.90885800939638));
#161743=CARTESIAN_POINT('Ctrl Pts',(-18.932821038579,-16.8442984017036,
4.90092860974278));
#161744=CARTESIAN_POINT('Ctrl Pts',(-18.948457091729,-16.8458319229441,
4.90000298475811));
#161745=CARTESIAN_POINT('Ctrl Pts',(-18.9720878358004,-16.848415400701,
4.89859414442555));
#161746=CARTESIAN_POINT('Ctrl Pts',(-18.9800961951671,-16.8493372491194,
4.89811496295466));
#161747=CARTESIAN_POINT('Ctrl Pts',(-18.9944375160585,-16.8510711425286,
4.89725366733439));
#161748=CARTESIAN_POINT('Ctrl Pts',(-19.0007724680078,-16.8518661440613,
4.89687209560441));
#161749=CARTESIAN_POINT('Ctrl Pts',(-19.0142071226201,-16.8536138864864,
4.89606048385466));
#161750=CARTESIAN_POINT('Ctrl Pts',(-19.0213057664531,-16.8545740281115,
4.8956302141999));
#161751=CARTESIAN_POINT('Ctrl Pts',(-19.0402901067684,-16.8572399781245,
4.89447563006658));
#161752=CARTESIAN_POINT('Ctrl Pts',(-19.0521662611979,-16.8590108935598,
4.89374926375494));
#161753=CARTESIAN_POINT('Ctrl Pts',(-19.1099184349702,-16.8681255180905,
4.89019666408887));
#161754=CARTESIAN_POINT('Ctrl Pts',(-19.1555563695704,-16.8768765770421,
4.88732612215798));
#161755=CARTESIAN_POINT('Ctrl Pts',(-19.3657128989447,-16.9243927411314,
4.87380333280703));
#161756=CARTESIAN_POINT('Ctrl Pts',(-19.5254827714283,-16.9812665585503,
4.86258058250836));
#161757=CARTESIAN_POINT('Ctrl Pts',(-19.7656361258193,-17.1007116078515,
4.84491085389191));
#161758=CARTESIAN_POINT('Ctrl Pts',(-19.8513036570371,-17.1511171540428,
4.83844240407972));
#161759=CARTESIAN_POINT('Ctrl Pts',(-19.9411074612132,-17.2128408968588,
4.83170982320692));
#161760=CARTESIAN_POINT('Ctrl Pts',(-19.9490518323792,-17.2183818581448,
4.8311147213328));
#161761=CARTESIAN_POINT('Ctrl Pts',(-19.9607272799889,-17.2266448182095,
4.83024118945379));
#161762=CARTESIAN_POINT('Ctrl Pts',(-19.964487796717,-17.2293247241968,
4.82995999962427));
#161763=CARTESIAN_POINT('Ctrl Pts',(-19.971058383223,-17.2340396995757,
4.82946902054066));
#161764=CARTESIAN_POINT('Ctrl Pts',(-19.9738722480909,-17.2360693934808,
4.82925886674482));
#161765=CARTESIAN_POINT('Ctrl Pts',(-19.976694523198,-17.2381157208593,
4.82904819919936));
#161766=CARTESIAN_POINT('Ctrl Pts',(-19.9767078753003,-17.2381254022133,
4.82904720253976));
#161767=CARTESIAN_POINT('Ctrl Pts',(-19.9767343421635,-17.2381445933015,
4.8290452269417));
#161768=CARTESIAN_POINT('Ctrl Pts',(-19.9767474569972,-17.23815410308,4.82904424799773));
#161769=CARTESIAN_POINT('Ctrl Pts',(-19.9767734550326,-17.2381729551324,
4.82904230740449));
#161770=CARTESIAN_POINT('Ctrl Pts',(-19.9767863381139,-17.2381822973108,
4.82904134576413));
#161771=CARTESIAN_POINT('Ctrl Pts',(-19.9768118775577,-17.2382008177018,
4.82903943941112));
#161772=CARTESIAN_POINT('Ctrl Pts',(-19.9768245340366,-17.238209995991,
4.82903849468971));
#161773=CARTESIAN_POINT('Ctrl Pts',(-19.9768496251652,-17.2382281921263,
4.82903662180938));
#161774=CARTESIAN_POINT('Ctrl Pts',(-19.9768620599652,-17.238237210074,
4.82903569363918));
#161775=CARTESIAN_POINT('Ctrl Pts',(-19.9768867133356,-17.2382550895651,
4.82903385344305));
#161776=CARTESIAN_POINT('Ctrl Pts',(-19.9768989316573,-17.238263950921,
4.82903294143562));
#161777=CARTESIAN_POINT('Ctrl Pts',(-19.9769231561415,-17.2382815201594,
4.82903113326101));
#161778=CARTESIAN_POINT('Ctrl Pts',(-19.9769351624872,-17.2382902281679,
4.82903023708009));
#161779=CARTESIAN_POINT('Ctrl Pts',(-19.9769589684708,-17.2383074946448,
4.82902846015136));
#161780=CARTESIAN_POINT('Ctrl Pts',(-19.9769707678798,-17.2383160529407,
4.82902757942057));
#161781=CARTESIAN_POINT('Ctrl Pts',(-19.9769941631387,-17.2383330222566,
4.82902583315689));
#161782=CARTESIAN_POINT('Ctrl Pts',(-19.977005759516,-17.2383414336527,
4.82902496758456));
#161783=CARTESIAN_POINT('Ctrl Pts',(-19.9770287548157,-17.2383581135781,
4.82902325118198));
#161784=CARTESIAN_POINT('Ctrl Pts',(-19.977040153179,-17.2383663816956,
4.82902240039339));
#161785=CARTESIAN_POINT('Ctrl Pts',(-19.9770627555768,-17.238382777313,
4.82902071332475));
#161786=CARTESIAN_POINT('Ctrl Pts',(-19.9770739598371,-17.2383909049709,
4.82901987702778));
#161787=CARTESIAN_POINT('Ctrl Pts',(-19.9770961785962,-17.2384070229647,
4.8290182186013));
#161788=CARTESIAN_POINT('Ctrl Pts',(-19.9771071930207,-17.2384150132412,
4.82901739647727));
#161789=CARTESIAN_POINT('Ctrl Pts',(-19.9771290361249,-17.2384308593692,
4.82901576609667));
#161790=CARTESIAN_POINT('Ctrl Pts',(-19.9771398647644,-17.2384387151863,
4.82901495784305));
#161791=CARTESIAN_POINT('Ctrl Pts',(-19.9771613400607,-17.2384542951087,
4.82901335492229));
#161792=CARTESIAN_POINT('Ctrl Pts',(-19.9771719867371,-17.238462019223,
4.82901256025364));
#161793=CARTESIAN_POINT('Ctrl Pts',(-19.9771931024015,-17.23847733884,4.82901098418214));
#161794=CARTESIAN_POINT('Ctrl Pts',(-19.9772035711358,-17.2384849341536,
4.82901020279816));
#161795=CARTESIAN_POINT('Ctrl Pts',(-19.9772237352472,-17.2384995639739,
4.82900869775636));
#161796=CARTESIAN_POINT('Ctrl Pts',(-19.9772334306857,-17.2385065985044,
4.82900797409373));
#161797=CARTESIAN_POINT('Ctrl Pts',(-19.9772527849239,-17.2385206412328,
4.82900652950578));
#161798=CARTESIAN_POINT('Ctrl Pts',(-19.9772624437172,-17.2385276494251,
4.82900580858092));
#161799=CARTESIAN_POINT('Ctrl Pts',(-19.9772817254746,-17.2385416400617,
4.82900436940807));
#161800=CARTESIAN_POINT('Ctrl Pts',(-19.9772913482979,-17.2385486224031,
4.82900365117055));
#161801=CARTESIAN_POINT('Ctrl Pts',(-19.9773105568827,-17.2385625604404,
4.82900221746436));
#161802=CARTESIAN_POINT('Ctrl Pts',(-19.9773201434178,-17.2385695166971,
4.82900150193792));
#161803=CARTESIAN_POINT('Ctrl Pts',(-19.9773392810324,-17.2385834037278,
4.82900007353395));
#161804=CARTESIAN_POINT('Ctrl Pts',(-19.9773488318792,-17.2385903343322,
4.82899936067377));
#161805=CARTESIAN_POINT('Ctrl Pts',(-19.9806516390466,-17.2409870697267,
4.82875284478144));
#161806=CARTESIAN_POINT('Ctrl Pts',(-19.9839380300116,-17.2433863870169,
4.82850770451671));
#161807=CARTESIAN_POINT('Ctrl Pts',(-19.9907317717478,-17.2483764304588,
4.82800120773937));
#161808=CARTESIAN_POINT('Ctrl Pts',(-19.994238080825,-17.2509685501977,
4.82773994794951));
#161809=CARTESIAN_POINT('Ctrl Pts',(-20.0031347309729,-17.257588211032,
4.82707735269185));
#161810=CARTESIAN_POINT('Ctrl Pts',(-20.0085139694754,-17.2616306852538,
4.82667701072026));
#161811=CARTESIAN_POINT('Ctrl Pts',(-20.0239756832433,-17.2733658629342,
4.8255268345415));
#161812=CARTESIAN_POINT('Ctrl Pts',(-20.0340086051042,-17.2811237411081,
4.82478116518051));
#161813=CARTESIAN_POINT('Ctrl Pts',(-20.068204360882,-17.308059818423,4.82223963905115));
#161814=CARTESIAN_POINT('Ctrl Pts',(-20.0920183841967,-17.327676492657,
4.82046966123372));
#161815=CARTESIAN_POINT('Ctrl Pts',(-20.2108685129124,-17.4300202812137,
4.81158694628816));
#161816=CARTESIAN_POINT('Ctrl Pts',(-20.298818187395,-17.5205979337703,
4.80483692030293));
#161817=CARTESIAN_POINT('Ctrl Pts',(-20.4064864810014,-17.6533487062865,
4.79553206515607));
#161818=CARTESIAN_POINT('Ctrl Pts',(-20.4336602988542,-17.6891219737193,
4.79307711846138));
#161819=CARTESIAN_POINT('Ctrl Pts',(-20.5143634568165,-17.8026920858774,
4.78537988888213));
#161820=CARTESIAN_POINT('Ctrl Pts',(-20.5638360196076,-17.883215804101,
4.78005127147159));
#161821=CARTESIAN_POINT('Ctrl Pts',(-20.6142037020075,-17.9790075371923,
4.77370715362279));
#161822=CARTESIAN_POINT('Ctrl Pts',(-20.6205202468542,-17.9913118932795,
4.77289231173098));
#161823=CARTESIAN_POINT('Ctrl Pts',(-20.6304430559604,-18.0111163872429,
4.77158046959409));
#161824=CARTESIAN_POINT('Ctrl Pts',(-20.6341265157695,-18.0185775563508,
4.7710861751603));
#161825=CARTESIAN_POINT('Ctrl Pts',(-20.640580691291,-18.031847575125,4.77020684443803));
#161826=CARTESIAN_POINT('Ctrl Pts',(-20.6433690996284,-18.0376477388998,
4.76982243041251));
#161827=CARTESIAN_POINT('Ctrl Pts',(-20.649116064526,-18.0497429196095,
4.76902062071427));
#161828=CARTESIAN_POINT('Ctrl Pts',(-20.6520701269773,-18.0560399752663,
4.76860307497836));
#161829=CARTESIAN_POINT('Ctrl Pts',(-20.6596449323438,-18.0723960386983,
4.76751821072469));
#161830=CARTESIAN_POINT('Ctrl Pts',(-20.6642178631581,-18.08247683892,4.7668492541554));
#161831=CARTESIAN_POINT('Ctrl Pts',(-20.6835890262932,-18.1260855208706,
4.76395371378824));
#161832=CARTESIAN_POINT('Ctrl Pts',(-20.697593594552,-18.1599570527064,
4.76170026312353));
#161833=CARTESIAN_POINT('Ctrl Pts',(-20.7147526103457,-18.2047145499013,
4.7587149690439));
#161834=CARTESIAN_POINT('Ctrl Pts',(-20.7187091228593,-18.2152869608762,
4.75800926474269));
#161835=CARTESIAN_POINT('Ctrl Pts',(-20.7225805756119,-18.2258896128692,
4.75730100916854));
#161836=CARTESIAN_POINT('Ctrl Pts',(-20.7225805465488,-18.2258895332749,
4.53222344315201));
#161837=CARTESIAN_POINT('Ctrl Pts',(-20.7132341698751,-18.2002928456002,
4.53397165328878));
#161838=CARTESIAN_POINT('Ctrl Pts',(-20.7033922852884,-18.1748730681182,
4.53573282534905));
#161839=CARTESIAN_POINT('Ctrl Pts',(-20.6611690694518,-18.0717793604969,
4.54297361842479));
#161840=CARTESIAN_POINT('Ctrl Pts',(-20.6246658403405,-17.9958878264983,
4.54853816195081));
#161841=CARTESIAN_POINT('Ctrl Pts',(-20.5387822929292,-17.8415962180799,
4.56020410800601));
#161842=CARTESIAN_POINT('Ctrl Pts',(-20.4885726480977,-17.7638447041638,
4.56629230712149));
#161843=CARTESIAN_POINT('Ctrl Pts',(-20.4146871476279,-17.6643787788858,
4.57415758382117));
#161844=CARTESIAN_POINT('Ctrl Pts',(-20.3953759382021,-17.6395565026307,
4.57612685398926));
#161845=CARTESIAN_POINT('Ctrl Pts',(-20.3709929261639,-17.6096161115965,
4.57850089209391));
#161846=CARTESIAN_POINT('Ctrl Pts',(-20.3664398639034,-17.6040829260377,
4.57893957344197));
#161847=CARTESIAN_POINT('Ctrl Pts',(-20.3592417851384,-17.5954253078551,
4.57962572993124));
#161848=CARTESIAN_POINT('Ctrl Pts',(-20.3566157000718,-17.5922853071087,
4.57987454040405));
#161849=CARTESIAN_POINT('Ctrl Pts',(-20.3516794645867,-17.5864177337804,
4.58033935590371));
#161850=CARTESIAN_POINT('Ctrl Pts',(-20.3493715402575,-17.5836884261612,
4.58055551029482));
#161851=CARTESIAN_POINT('Ctrl Pts',(-20.3440734337965,-17.5774550729701,
4.58104906821316));
#161852=CARTESIAN_POINT('Ctrl Pts',(-20.3410787255451,-17.5739549392488,
4.58132613415012));
#161853=CARTESIAN_POINT('Ctrl Pts',(-20.3332092480032,-17.5648178495249,
4.58204930169394));
#161854=CARTESIAN_POINT('Ctrl Pts',(-20.3283160476508,-17.5591967542389,
4.58249407838711));
#161855=CARTESIAN_POINT('Ctrl Pts',(-20.2954625318247,-17.5218560713192,
4.58544887372895));
#161856=CARTESIAN_POINT('Ctrl Pts',(-20.2665849052554,-17.4909521077891,
4.58789516401588));
#161857=CARTESIAN_POINT('Ctrl Pts',(-20.18430508153,-17.4080249723628,4.59453070354902));
#161858=CARTESIAN_POINT('Ctrl Pts',(-20.1290503460957,-17.3579235472439,
4.59862316268444));
#161859=CARTESIAN_POINT('Ctrl Pts',(-20.0017406212783,-17.2541880063822,
4.60757114625466));
#161860=CARTESIAN_POINT('Ctrl Pts',(-19.928688100799,-17.2020137225569,
4.61240567856214));
#161861=CARTESIAN_POINT('Ctrl Pts',(-19.7927399723901,-17.1174098734573,
4.62121398285934));
#161862=CARTESIAN_POINT('Ctrl Pts',(-19.7311161795932,-17.0832010766469,
4.62514337858843));
#161863=CARTESIAN_POINT('Ctrl Pts',(-19.6436970962353,-17.0402291360845,
4.63071709143391));
#161864=CARTESIAN_POINT('Ctrl Pts',(-19.6192644837784,-17.0287934731523,
4.6322745660965));
#161865=CARTESIAN_POINT('Ctrl Pts',(-19.5765470545152,-17.009786110035,
4.63500129709143));
#161866=CARTESIAN_POINT('Ctrl Pts',(-19.5583619685493,-17.0019980412646,
4.63616320377414));
#161867=CARTESIAN_POINT('Ctrl Pts',(-19.5320226890888,-16.9911520855306,
4.63784880855595));
#161868=CARTESIAN_POINT('Ctrl Pts',(-19.5239542558002,-16.9878877256442,
4.63836551344969));
#161869=CARTESIAN_POINT('Ctrl Pts',(-19.5098224391324,-16.9822713799362,
4.63927123937356));
#161870=CARTESIAN_POINT('Ctrl Pts',(-19.5037678830984,-16.9798973914996,
4.63965951291637));
#161871=CARTESIAN_POINT('Ctrl Pts',(-19.4921132355662,-16.9753894576432,
4.64040739481024));
#161872=CARTESIAN_POINT('Ctrl Pts',(-19.4865148256578,-16.973251317091,
4.64076685768586));
#161873=CARTESIAN_POINT('Ctrl Pts',(-19.4718422547873,-16.9677188534331,
4.64170954464167));
#161874=CARTESIAN_POINT('Ctrl Pts',(-19.46275381587,-16.9643630279792,4.64229404985813));
#161875=CARTESIAN_POINT('Ctrl Pts',(-19.431217001625,-16.9529637132039,
4.64432449566297));
#161876=CARTESIAN_POINT('Ctrl Pts',(-19.4086566245709,-16.945237435757,
4.64578090473388));
#161877=CARTESIAN_POINT('Ctrl Pts',(-19.2347577410227,-16.8889459198539,
4.65704092704006));
#161878=CARTESIAN_POINT('Ctrl Pts',(-19.0785398342249,-16.8571909180743,
4.66740835014237));
#161879=CARTESIAN_POINT('Ctrl Pts',(-18.7874110144881,-16.8314749848445,
4.68671882997158));
#161880=CARTESIAN_POINT('Ctrl Pts',(-18.6537237659806,-16.8323203358347,
4.69556321698931));
#161881=CARTESIAN_POINT('Ctrl Pts',(-18.5090891374847,-16.8469471982232,
4.70457890295002));
#161882=CARTESIAN_POINT('Ctrl Pts',(-18.4971935837579,-16.8482521703523,
4.70531613825132));
#161883=CARTESIAN_POINT('Ctrl Pts',(-18.4803117678559,-16.850249156788,
4.70635572617602));
#161884=CARTESIAN_POINT('Ctrl Pts',(-18.4753161756283,-16.8508581660727,
4.70666252461021));
#161885=CARTESIAN_POINT('Ctrl Pts',(-18.4667158674537,-16.8519377611493,
4.7071892133745));
#161886=CARTESIAN_POINT('Ctrl Pts',(-18.4631101202749,-16.8523998265388,
4.70740957988198));
#161887=CARTESIAN_POINT('Ctrl Pts',(-18.456125210662,-16.8533132145747,
4.70783556917243));
#161888=CARTESIAN_POINT('Ctrl Pts',(-18.452745948205,-16.8537634116723,
4.70804125665595));
#161889=CARTESIAN_POINT('Ctrl Pts',(-18.4436401179133,-16.8549989154241,
4.70859445284494));
#161890=CARTESIAN_POINT('Ctrl Pts',(-18.4379156058049,-16.8557995221983,
4.70894110371066));
#161891=CARTESIAN_POINT('Ctrl Pts',(-18.4167307325724,-16.858850866087,
4.71022003850795));
#161892=CARTESIAN_POINT('Ctrl Pts',(-18.4012917160183,-16.8612493418011,
4.71114434419333));
#161893=CARTESIAN_POINT('Ctrl Pts',(-18.2518420397532,-16.886164033899,
4.72002861835446));
#161894=CARTESIAN_POINT('Ctrl Pts',(-18.1202473313518,-16.9213664980603,
4.72737209707388));
#161895=CARTESIAN_POINT('Ctrl Pts',(-17.8474697539941,-17.0233050659381,
4.74318579733434));
#161896=CARTESIAN_POINT('Ctrl Pts',(-17.7084584309003,-17.0934906421178,
4.75164275711871));
#161897=CARTESIAN_POINT('Ctrl Pts',(-17.5605541346376,-17.1898517935364,
4.76192306858276));
#161898=CARTESIAN_POINT('Ctrl Pts',(-17.5429075551342,-17.2017313806992,
4.76317135723129));
#161899=CARTESIAN_POINT('Ctrl Pts',(-17.5180627038245,-17.2190065480735,
4.76496143173987));
#161900=CARTESIAN_POINT('Ctrl Pts',(-17.5107148152778,-17.2241854365431,
4.76549497998513));
#161901=CARTESIAN_POINT('Ctrl Pts',(-17.4980927009536,-17.2332025440944,
4.76641876835455));
#161902=CARTESIAN_POINT('Ctrl Pts',(-17.4928027806735,-17.2370186567979,
4.76680815426463));
#161903=CARTESIAN_POINT('Ctrl Pts',(-17.4827059284014,-17.2443736427606,
4.76755569184351));
#161904=CARTESIAN_POINT('Ctrl Pts',(-17.4778961553104,-17.2479085236472,
4.76791368611938));
#161905=CARTESIAN_POINT('Ctrl Pts',(-17.4654235125766,-17.2571566279455,
4.76884701308591));
#161906=CARTESIAN_POINT('Ctrl Pts',(-17.4577843351987,-17.2629014438258,
4.76942357782286));
#161907=CARTESIAN_POINT('Ctrl Pts',(-17.4318448287081,-17.2826849034036,
4.77139842544028));
#161908=CARTESIAN_POINT('Ctrl Pts',(-17.4137356461174,-17.2969704076124,
4.77280642563418));
#161909=CARTESIAN_POINT('Ctrl Pts',(-17.2606433229297,-17.4218496533437,
4.78496779960191));
#161910=CARTESIAN_POINT('Ctrl Pts',(-17.1396036025273,-17.5484270415927,
4.79641594462189));
#161911=CARTESIAN_POINT('Ctrl Pts',(-16.9831336496416,-17.7587488697623,
4.81373668220938));
#161912=CARTESIAN_POINT('Ctrl Pts',(-16.9352031781223,-17.832306664799,
4.81951870117531));
#161913=CARTESIAN_POINT('Ctrl Pts',(-16.873244462909,-17.9416922878681,
4.82754620714642));
#161914=CARTESIAN_POINT('Ctrl Pts',(-16.8554092272129,-17.9752554245049,
4.82993665574684));
#161915=CARTESIAN_POINT('Ctrl Pts',(-16.8351098187183,-18.0160712838823,
4.83274182588761));
#161916=CARTESIAN_POINT('Ctrl Pts',(-16.8317700583309,-18.022877976134,
4.8332062963631));
#161917=CARTESIAN_POINT('Ctrl Pts',(-16.826643889089,-18.0334690122416,
4.83392366556618));
#161918=CARTESIAN_POINT('Ctrl Pts',(-16.8248320506798,-18.0372408779958,
4.83417810337687));
#161919=CARTESIAN_POINT('Ctrl Pts',(-16.8214979335923,-18.0442348625049,
4.83464792936058));
#161920=CARTESIAN_POINT('Ctrl Pts',(-16.8199726200361,-18.0474554251367,
4.83486350046578));
#161921=CARTESIAN_POINT('Ctrl Pts',(-16.816549249544,-18.0547309966319,
4.83534876790478));
#161922=CARTESIAN_POINT('Ctrl Pts',(-16.8146559253095,-18.0587881725892,
4.83561817017496));
#161923=CARTESIAN_POINT('Ctrl Pts',(-16.809124752865,-18.0707396324551,
4.83640831557005));
#161924=CARTESIAN_POINT('Ctrl Pts',(-16.8055225852273,-18.0786504600029,
4.83692691077849));
#161925=CARTESIAN_POINT('Ctrl Pts',(-16.7804077321024,-18.1347190292277,
4.84057293604675));
#161926=CARTESIAN_POINT('Ctrl Pts',(-16.7606507745182,-18.1836480249946,
4.84360127844008));
#161927=CARTESIAN_POINT('Ctrl Pts',(-16.73735532374,-18.2481884793583,4.84746205677662));
#161928=CARTESIAN_POINT('Ctrl Pts',(-16.7321376863721,-18.2631691681107,
4.84834901037666));
#161929=CARTESIAN_POINT('Ctrl Pts',(-16.7109324729106,-18.3263295177812,
4.85205540294843));
#161930=CARTESIAN_POINT('Ctrl Pts',(-16.6965116118114,-18.3750189036801,
4.85483249117402));
#161931=CARTESIAN_POINT('Ctrl Pts',(-16.6565766058816,-18.5301337781672,
4.86355328254866));
#161932=CARTESIAN_POINT('Ctrl Pts',(-16.6375535424663,-18.6380407012192,
4.86944421280929));
#161933=CARTESIAN_POINT('Ctrl Pts',(-16.6216105990453,-18.8018505503604,
4.87859515234573));
#161934=CARTESIAN_POINT('Ctrl Pts',(-16.618415026896,-18.8569557334196,
4.88170645412652));
#161935=CARTESIAN_POINT('Ctrl Pts',(-16.6167287794547,-18.9464533285306,
4.8868561722034));
#161936=CARTESIAN_POINT('Ctrl Pts',(-16.6169173843099,-18.9807956270069,
4.88885508612901));
#161937=CARTESIAN_POINT('Ctrl Pts',(-16.6182634673156,-19.0259245254794,
4.8915177937537));
#161938=CARTESIAN_POINT('Ctrl Pts',(-16.618668626598,-19.0367294832906,
4.89215801258617));
#161939=CARTESIAN_POINT('Ctrl Pts',(-16.6194678543697,-19.0544226581958,
4.89321097988307));
#161940=CARTESIAN_POINT('Ctrl Pts',(-16.6198128589424,-19.0613129757628,
4.8936221855651));
#161941=CARTESIAN_POINT('Ctrl Pts',(-16.620545930046,-19.0746481990425,
4.89442028063306));
#161942=CARTESIAN_POINT('Ctrl Pts',(-16.6209298132785,-19.0810932650825,
4.89480703430517));
#161943=CARTESIAN_POINT('Ctrl Pts',(-16.6218843407219,-19.0959718411295,
4.89570227454407));
#161944=CARTESIAN_POINT('Ctrl Pts',(-16.6224760212405,-19.104403848681,
4.89621141660208));
#161945=CARTESIAN_POINT('Ctrl Pts',(-16.6242032953423,-19.1270739123451,
4.89758519790726));
#161946=CARTESIAN_POINT('Ctrl Pts',(-16.6254324974504,-19.1413042029773,
4.89845276172805));
#161947=CARTESIAN_POINT('Ctrl Pts',(-16.6403655321411,-19.2959165237637,
4.90793723006079));
#161948=CARTESIAN_POINT('Ctrl Pts',(-16.6679197445768,-19.4345794148788,
4.91700377262712));
#161949=CARTESIAN_POINT('Ctrl Pts',(-16.7372255039126,-19.6618705569734,
4.93263656447653));
#161950=CARTESIAN_POINT('Ctrl Pts',(-16.7717001889072,-19.7522526135086,
4.93906371547369));
#161951=CARTESIAN_POINT('Ctrl Pts',(-16.832768076071,-19.8844185044703,
4.94856446621622));
#161952=CARTESIAN_POINT('Ctrl Pts',(-16.8548461434578,-19.9281498414661,
4.95172468780281));
#161953=CARTESIAN_POINT('Ctrl Pts',(-16.8910600140968,-19.9940894445889,
4.95647524086287));
#161954=CARTESIAN_POINT('Ctrl Pts',(-16.9041251107082,-20.0168644225433,
4.95811320058636));
#161955=CARTESIAN_POINT('Ctrl Pts',(-16.9210830106382,-20.0451910522236,
4.96014122342321));
#161956=CARTESIAN_POINT('Ctrl Pts',(-16.9245826731284,-20.0509738973456,
4.9605547499238));
#161957=CARTESIAN_POINT('Ctrl Pts',(-16.930199125645,-20.0601549675977,
4.96121037107058));
#161958=CARTESIAN_POINT('Ctrl Pts',(-16.9322979273812,-20.0635640641327,
4.96145361400821));
#161959=CARTESIAN_POINT('Ctrl Pts',(-16.9362987504488,-20.0700215235412,
4.96191394807351));
#161960=CARTESIAN_POINT('Ctrl Pts',(-16.9381988377285,-20.0730709591624,
4.96213115415988));
#161961=CARTESIAN_POINT('Ctrl Pts',(-16.9425927711319,-20.080082913768,
4.96263021362789));
#161962=CARTESIAN_POINT('Ctrl Pts',(-16.9450920042347,-20.0840420061228,
4.962911707208));
#161963=CARTESIAN_POINT('Ctrl Pts',(-16.9518304867256,-20.0946385481305,
4.96366445104067));
#161964=CARTESIAN_POINT('Ctrl Pts',(-16.9560937213901,-20.1012607600365,
4.96413415680802));
#161965=CARTESIAN_POINT('Ctrl Pts',(-16.9884341288233,-20.150885443716,
4.9676498060224));
#161966=CARTESIAN_POINT('Ctrl Pts',(-17.0180332723692,-20.1928809883391,
4.97060141188804));
#161967=CARTESIAN_POINT('Ctrl Pts',(-17.0626669549787,-20.2515516526043,
4.97475416758939));
#161968=CARTESIAN_POINT('Ctrl Pts',(-17.076481924843,-20.2691266167594,
4.97600207142634));
#161969=CARTESIAN_POINT('Ctrl Pts',(-17.119514681734,-20.3221219415788,
4.97978792889078));
#161970=CARTESIAN_POINT('Ctrl Pts',(-17.149609077374,-20.3568140883186,
4.98229853088526));
#161971=CARTESIAN_POINT('Ctrl Pts',(-17.2551134179209,-20.4707301954672,
4.99075196207313));
#161972=CARTESIAN_POINT('Ctrl Pts',(-17.3355222207308,-20.5450806466628,
4.99664017659348));
#161973=CARTESIAN_POINT('Ctrl Pts',(-17.4645497862562,-20.6470582914016,
5.00578480191334));
#161974=CARTESIAN_POINT('Ctrl Pts',(-17.5091039392043,-20.6795287121224,
5.00889248403912));
#161975=CARTESIAN_POINT('Ctrl Pts',(-17.5833664464427,-20.7293318583208,
5.01403674499457));
#161976=CARTESIAN_POINT('Ctrl Pts',(-17.6123200062058,-20.7477449440492,
5.01603393114697));
#161977=CARTESIAN_POINT('Ctrl Pts',(-17.6509662137625,-20.7710227194652,
5.01869466319579));
#161978=CARTESIAN_POINT('Ctrl Pts',(-17.6602678299966,-20.7765287217809,
5.01933467884781));
#161979=CARTESIAN_POINT('Ctrl Pts',(-17.6755739798853,-20.7854314672858,
5.02038739706774));
#161980=CARTESIAN_POINT('Ctrl Pts',(-17.6815537456503,-20.7888705630128,
5.02079855828543));
#161981=CARTESIAN_POINT('Ctrl Pts',(-17.6931629868897,-20.7954719967072,
5.02159662786776));
#161982=CARTESIAN_POINT('Ctrl Pts',(-17.6987903379179,-20.798637930024,
5.02198340084067));
#161983=CARTESIAN_POINT('Ctrl Pts',(-17.7118194744673,-20.8058898171546,
5.02287877434169));
#161984=CARTESIAN_POINT('Ctrl Pts',(-17.7192313926116,-20.809957252239,
5.02338803097568));
#161985=CARTESIAN_POINT('Ctrl Pts',(-17.7392356903843,-20.8207795918798,
5.0247623219171));
#161986=CARTESIAN_POINT('Ctrl Pts',(-17.7518722593776,-20.8274514870012,
5.02563028417575));
#161987=CARTESIAN_POINT('Ctrl Pts',(-17.8684343403599,-20.8874931911693,
5.03363629200761));
#161988=CARTESIAN_POINT('Ctrl Pts',(-17.9765265204829,-20.9322938996647,
5.04107600485072));
#161989=CARTESIAN_POINT('Ctrl Pts',(-18.2426389377099,-21.0176017536676,
5.05932949857795));
#161990=CARTESIAN_POINT('Ctrl Pts',(-18.402733842658,-21.0492384447102,
5.07028316856227));
#161991=CARTESIAN_POINT('Ctrl Pts',(-18.5973543192778,-21.0648366936974,
5.08269036370956));
#161992=CARTESIAN_POINT('Ctrl Pts',(-18.6298954305007,-21.0666899170629,
5.0847329084645));
#161993=CARTESIAN_POINT('Ctrl Pts',(-18.669709243479,-21.068035961258,5.08718259740535));
#161994=CARTESIAN_POINT('Ctrl Pts',(-18.6769514839577,-21.0682435968064,
5.08762620712772));
#161995=CARTESIAN_POINT('Ctrl Pts',(-18.6883044942779,-21.0685107653795,
5.08831833651239));
#161996=CARTESIAN_POINT('Ctrl Pts',(-18.692414534851,-21.0685955090576,
5.08856822950109));
#161997=CARTESIAN_POINT('Ctrl Pts',(-18.7000959912316,-21.0687315076159,
5.08903397575754));
#161998=CARTESIAN_POINT('Ctrl Pts',(-18.7036672506855,-21.0687856957413,
5.08924998492894));
#161999=CARTESIAN_POINT('Ctrl Pts',(-18.7118178866375,-21.0688887372833,
5.08974179744461));
#162000=CARTESIAN_POINT('Ctrl Pts',(-18.7163972862393,-21.0689317696994,
5.09001727221514));
#162001=CARTESIAN_POINT('Ctrl Pts',(-18.7304669815236,-21.0690183239641,
5.09086113069955));
#162002=CARTESIAN_POINT('Ctrl Pts',(-18.739957609618,-21.0690128910078,
5.09142684615873));
#162003=CARTESIAN_POINT('Ctrl Pts',(-18.8248630376806,-21.0683933063672,
5.09645906364571));
#162004=CARTESIAN_POINT('Ctrl Pts',(-18.9002035832334,-21.0638133558985,
5.10072176045197));
#162005=CARTESIAN_POINT('Ctrl Pts',(-19.0179674183209,-21.0503110439731,
5.10728418536582));
#162006=CARTESIAN_POINT('Ctrl Pts',(-19.06062951064,-21.044094664851,5.10964041612543));
#162007=CARTESIAN_POINT('Ctrl Pts',(-19.2107236004419,-21.0175206389198,
5.11793913118044));
#162008=CARTESIAN_POINT('Ctrl Pts',(-19.3167349574163,-20.9901511189904,
5.12382599657494));
#162009=CARTESIAN_POINT('Ctrl Pts',(-19.4722607396144,-20.9368662105857,
5.13296748542311));
#162010=CARTESIAN_POINT('Ctrl Pts',(-19.5236475170903,-20.9169882818635,
5.13607336980315));
#162011=CARTESIAN_POINT('Ctrl Pts',(-19.6056757259783,-20.8815197605387,
5.14121492016582));
#162012=CARTESIAN_POINT('Ctrl Pts',(-19.6368163463106,-20.8671468680067,
5.14321124788829));
#162013=CARTESIAN_POINT('Ctrl Pts',(-19.6772925860797,-20.8472585300596,
5.14587099834465));
#162014=CARTESIAN_POINT('Ctrl Pts',(-19.686955487947,-20.8424183743692,
5.14651091298803));
#162015=CARTESIAN_POINT('Ctrl Pts',(-19.702724319387,-20.8343681290028,
5.14756350738441));
#162016=CARTESIAN_POINT('Ctrl Pts',(-19.7088524441597,-20.8312017694866,
5.14797464649899));
#162017=CARTESIAN_POINT('Ctrl Pts',(-19.7206868542345,-20.825013546177,
5.14877270342908));
#162018=CARTESIAN_POINT('Ctrl Pts',(-19.7263950103721,-20.8219954102718,
5.14915948601311));
#162019=CARTESIAN_POINT('Ctrl Pts',(-19.7395460668224,-20.8149647350969,
5.15005492583848));
#162020=CARTESIAN_POINT('Ctrl Pts',(-19.7469788757128,-20.810933643473,
5.15056423949151));
#162021=CARTESIAN_POINT('Ctrl Pts',(-19.7669102989717,-20.7999690476493,
5.15193878407969));
#162022=CARTESIAN_POINT('Ctrl Pts',(-19.7793630077215,-20.7929534087402,
5.15280694464777));
#162023=CARTESIAN_POINT('Ctrl Pts',(-19.8931567518873,-20.7273171444248,
5.16082820197506));
#162024=CARTESIAN_POINT('Ctrl Pts',(-19.9895263038909,-20.6605201751907,
5.16828430063986));
#162025=CARTESIAN_POINT('Ctrl Pts',(-20.2060270758592,-20.4822081569832,
5.18660646187756));
#162026=CARTESIAN_POINT('Ctrl Pts',(-20.3197247266999,-20.3640474464165,
5.19761444217112));
#162027=CARTESIAN_POINT('Ctrl Pts',(-20.4378770607849,-20.2087796611593,
5.21000238967397));
#162028=CARTESIAN_POINT('Ctrl Pts',(-20.4564901138432,-20.1831458939925,
5.21198632647171));
#162029=CARTESIAN_POINT('Ctrl Pts',(-20.4786101724612,-20.1511980331212,
5.21437553034573));
#162030=CARTESIAN_POINT('Ctrl Pts',(-20.4826683393949,-20.1452726506132,
5.21481521474922));
#162031=CARTESIAN_POINT('Ctrl Pts',(-20.4889941122921,-20.1359347323959,
5.2155025871682));
#162032=CARTESIAN_POINT('Ctrl Pts',(-20.4912820552425,-20.132536134023,
5.21575161821234));
#162033=CARTESIAN_POINT('Ctrl Pts',(-20.4955472989714,-20.1261605024198,
5.21621662195751));
#162034=CARTESIAN_POINT('Ctrl Pts',(-20.4975269050341,-20.1231851379675,
5.21643274535901));
#162035=CARTESIAN_POINT('Ctrl Pts',(-20.502037840125,-20.1163677955967,
5.21692594123951));
#162036=CARTESIAN_POINT('Ctrl Pts',(-20.5045641807298,-20.1125225764154,
5.21720267799311));
#162037=CARTESIAN_POINT('Ctrl Pts',(-20.5111396724453,-20.1024428919576,
5.21792442154061));
#162038=CARTESIAN_POINT('Ctrl Pts',(-20.5151685959468,-20.0961952191495,
5.21836811189974));
#162039=CARTESIAN_POINT('Ctrl Pts',(-20.541703546346,-20.0545675216058,
5.22130102276341));
#162040=CARTESIAN_POINT('Ctrl Pts',(-20.5631887144981,-20.0185441508521,
5.2237275831468));
#162041=CARTESIAN_POINT('Ctrl Pts',(-20.5941629419433,-19.9629179261417,
5.22734528599898));
#162042=CARTESIAN_POINT('Ctrl Pts',(-20.6044420996057,-19.9437699469114,
5.22856809922211));
#162043=CARTESIAN_POINT('Ctrl Pts',(-20.6222695281991,-19.909297667153,
5.23073557943077));
#162044=CARTESIAN_POINT('Ctrl Pts',(-20.629930472772,-19.8940341268798,
5.2316836403405));
#162045=CARTESIAN_POINT('Ctrl Pts',(-20.6957491953938,-19.7588419955118,
5.23999253111414));
#162046=CARTESIAN_POINT('Ctrl Pts',(-20.7426454644707,-19.6337617913964,
5.24709268312486));
#162047=CARTESIAN_POINT('Ctrl Pts',(-20.8031161820857,-19.410347912284,
5.25986486011464));
#162048=CARTESIAN_POINT('Ctrl Pts',(-20.822138260334,-19.3139387120578,
5.26540006226036));
#162049=CARTESIAN_POINT('Ctrl Pts',(-20.836236815956,-19.2020092178444,
5.27201867132379));
#162050=CARTESIAN_POINT('Ctrl Pts',(-20.8379188842745,-19.1874348137934,
5.27288400798651));
#162051=CARTESIAN_POINT('Ctrl Pts',(-20.840256748618,-19.1651464720422,
5.27421317025278));
#162052=CARTESIAN_POINT('Ctrl Pts',(-20.8410219635071,-19.1574442807824,
5.27467354796835));
#162053=CARTESIAN_POINT('Ctrl Pts',(-20.8422815028458,-19.1440185067431,
5.27547794502019));
#162054=CARTESIAN_POINT('Ctrl Pts',(-20.8427948029168,-19.1382967534845,
5.2758213631654));
#162055=CARTESIAN_POINT('Ctrl Pts',(-20.8438966146506,-19.1254264216854,
5.27659522283431));
#162056=CARTESIAN_POINT('Ctrl Pts',(-20.8444720950169,-19.1182768247099,
5.27702607003716));
#162057=CARTESIAN_POINT('Ctrl Pts',(-20.8459169689305,-19.0991085327299,
5.27818382203152));
#162058=CARTESIAN_POINT('Ctrl Pts',(-20.8467200884103,-19.0870852422579,
5.2789127983333));
#162059=CARTESIAN_POINT('Ctrl Pts',(-20.8498276623848,-19.0337143082532,
5.28216143303529));
#162060=CARTESIAN_POINT('Ctrl Pts',(-20.8510211084385,-18.9923134313835,
5.28471560481465));
#162061=CARTESIAN_POINT('Ctrl Pts',(-20.8509121655105,-18.7814276655538,
5.29790822725658));
#162062=CARTESIAN_POINT('Ctrl Pts',(-20.8304727786253,-18.6125948125901,
5.30913940085526));
#162063=CARTESIAN_POINT('Ctrl Pts',(-20.7716984107369,-18.3727973124188,
5.32541882928644));
#162064=CARTESIAN_POINT('Ctrl Pts',(-20.7491431140367,-18.298635775203,
5.33048901901233));
#162065=CARTESIAN_POINT('Ctrl Pts',(-20.7225805585332,-18.2258895660964,
5.33540095489714));
#162066=CARTESIAN_POINT('Origin',(-18.734,-18.952,0.));
#162067=CARTESIAN_POINT('',(-20.7225805737622,-18.2258896078036,6.35350377396604));
#162068=CARTESIAN_POINT('',(-20.7225805737622,-18.2258896078036,6.13370788795281));
#162069=CARTESIAN_POINT('',(-20.7225805737622,-18.2258896078036,0.));
#162070=CARTESIAN_POINT('',(-20.8509995791066,-18.9506650608985,6.31236863518829));
#162071=CARTESIAN_POINT('Ctrl Pts',(-20.7225805737622,-18.2258896078036,
6.35350377396603));
#162072=CARTESIAN_POINT('Ctrl Pts',(-20.7233987857641,-18.228130424778,
6.35336132124997));
#162073=CARTESIAN_POINT('Ctrl Pts',(-20.7242132152326,-18.2303726385444,
6.35321908228664));
#162074=CARTESIAN_POINT('Ctrl Pts',(-20.7362148871419,-18.2635894227243,
6.3511163241643));
#162075=CARTESIAN_POINT('Ctrl Pts',(-20.7466823514128,-18.2948214849994,
6.34919592571695));
#162076=CARTESIAN_POINT('Ctrl Pts',(-20.804402162798,-18.4813823304818,
6.33798821755311));
#162077=CARTESIAN_POINT('Ctrl Pts',(-20.8343919994919,-18.6414983883584,
6.3294064643659));
#162078=CARTESIAN_POINT('Ctrl Pts',(-20.8492292021156,-18.852470693199,
6.31782784890908));
#162079=CARTESIAN_POINT('Ctrl Pts',(-20.850968615029,-18.9015609936698,
6.31511813187666));
#162080=CARTESIAN_POINT('Ctrl Pts',(-20.8509995791066,-18.9506650608985,
6.31236863518829));
#162081=CARTESIAN_POINT('Ctrl Pts',(-20.850999580792,-18.950667736265,6.31236848538577));
#162082=CARTESIAN_POINT('Ctrl Pts',(-20.851043483142,-19.0204296415699,
6.30846228705901));
#162083=CARTESIAN_POINT('Ctrl Pts',(-20.8476391052175,-19.0901465311592,
6.3044787447757));
#162084=CARTESIAN_POINT('Ctrl Pts',(-20.8397874280136,-19.1698415376233,
6.29977974061186));
#162085=CARTESIAN_POINT('Ctrl Pts',(-20.838699830613,-19.1801101595302,
6.29917153797656));
#162086=CARTESIAN_POINT('Ctrl Pts',(-20.8367367427085,-19.1974337468722,
6.29814066915109));
#162087=CARTESIAN_POINT('Ctrl Pts',(-20.8359007542262,-19.2044930707003,
6.29771924246229));
#162088=CARTESIAN_POINT('Ctrl Pts',(-20.8342952243256,-19.2174897628251,
6.29694082323744));
#162089=CARTESIAN_POINT('Ctrl Pts',(-20.8335360182493,-19.2234283523007,
6.29658415929102));
#162090=CARTESIAN_POINT('Ctrl Pts',(-20.8319167098582,-19.2356813162761,
6.29584620337817));
#162091=CARTESIAN_POINT('Ctrl Pts',(-20.8310532669144,-19.2419951810888,
6.29546480933832));
#162092=CARTESIAN_POINT('Ctrl Pts',(-20.8290511037879,-19.256159157267,
6.29460664266265));
#162093=CARTESIAN_POINT('Ctrl Pts',(-20.827896748574,-19.2640069295245,
6.29412937965364));
#162094=CARTESIAN_POINT('Ctrl Pts',(-20.8248477368161,-19.2839559768024,
6.29291155896707));
#162095=CARTESIAN_POINT('Ctrl Pts',(-20.8228921293394,-19.2960475129605,
6.29216907962002));
#162096=CARTESIAN_POINT('Ctrl Pts',(-20.8108473634669,-19.3666285385382,
6.28780914956202));
#162097=CARTESIAN_POINT('Ctrl Pts',(-20.798407807303,-19.4246849952108,
6.28411753440282));
#162098=CARTESIAN_POINT('Ctrl Pts',(-20.7682289796244,-19.5413582338922,
6.27647858351458));
#162099=CARTESIAN_POINT('Ctrl Pts',(-20.750352624344,-19.5998825593458,
6.27253040362192));
#162100=CARTESIAN_POINT('Ctrl Pts',(-20.6757998924098,-19.8107896640081,
6.25791902873149));
#162101=CARTESIAN_POINT('Ctrl Pts',(-20.6041653868007,-19.9572800498515,
6.24697387471078));
#162102=CARTESIAN_POINT('Ctrl Pts',(-20.498817485321,-20.1216921367102,
6.2345635089915));
#162103=CARTESIAN_POINT('Ctrl Pts',(-20.4805198616982,-20.1488413001332,
6.23251162573885));
#162104=CARTESIAN_POINT('Ctrl Pts',(-20.4574056988078,-20.1814773001668,
6.23005231627239));
#162105=CARTESIAN_POINT('Ctrl Pts',(-20.4531820976744,-20.1873762798653,
6.22960809306921));
#162106=CARTESIAN_POINT('Ctrl Pts',(-20.446516599077,-20.1965853988361,
6.22891522043675));
#162107=CARTESIAN_POINT('Ctrl Pts',(-20.444095284521,-20.199910267461,6.22866519291995));
#162108=CARTESIAN_POINT('Ctrl Pts',(-20.439553433237,-20.2061089431634,
6.2281993298121));
#162109=CARTESIAN_POINT('Ctrl Pts',(-20.4374353375712,-20.2089844095676,
6.22798333750798));
#162110=CARTESIAN_POINT('Ctrl Pts',(-20.4325865241339,-20.2155322561536,
6.2274917365059));
#162111=CARTESIAN_POINT('Ctrl Pts',(-20.4298511743862,-20.219201143286,
6.22721645528447));
#162112=CARTESIAN_POINT('Ctrl Pts',(-20.4214167320953,-20.2304379232171,
6.22637377849424));
#162113=CARTESIAN_POINT('Ctrl Pts',(-20.4156786290726,-20.2379765734037,
6.22580904033915));
#162114=CARTESIAN_POINT('Ctrl Pts',(-20.3357810536373,-20.3414956833256,
6.21805867897201));
#162115=CARTESIAN_POINT('Ctrl Pts',(-20.2535455451829,-20.4309830144674,
6.21140581709675));
#162116=CARTESIAN_POINT('Ctrl Pts',(-20.0841705050021,-20.5861590206874,
6.19890604494905));
#162117=CARTESIAN_POINT('Ctrl Pts',(-19.9987512761304,-20.6531288356912,
6.1930651781268));
#162118=CARTESIAN_POINT('Ctrl Pts',(-19.8636984675659,-20.7431954412522,
6.18403046750809));
#162119=CARTESIAN_POINT('Ctrl Pts',(-19.8176879652415,-20.7714008681651,
6.18098566704922));
#162120=CARTESIAN_POINT('Ctrl Pts',(-19.7510779233441,-20.8088105799518,
6.1765884665442));
#162121=CARTESIAN_POINT('Ctrl Pts',(-19.7313300613595,-20.8194918276574,
6.17528622691319));
#162122=CARTESIAN_POINT('Ctrl Pts',(-19.6962437822886,-20.837754089413,
6.17297262699503));
#162123=CARTESIAN_POINT('Ctrl Pts',(-19.680976173762,-20.8454671064222,
6.17196591636279));
#162124=CARTESIAN_POINT('Ctrl Pts',(-19.6582589621574,-20.8566000935249,
6.17046734883786));
#162125=CARTESIAN_POINT('Ctrl Pts',(-19.6508800291644,-20.8601632934894,
6.16998049039768));
#162126=CARTESIAN_POINT('Ctrl Pts',(-19.6379488512007,-20.8663152827094,
6.16912704763187));
#162127=CARTESIAN_POINT('Ctrl Pts',(-19.6324056771298,-20.8689229940936,
6.16876112497135));
#162128=CARTESIAN_POINT('Ctrl Pts',(-19.621338875214,-20.8740706755956,
6.16803037806014));
#162129=CARTESIAN_POINT('Ctrl Pts',(-19.6158154687229,-20.8766109839063,
6.16766556987319));
#162130=CARTESIAN_POINT('Ctrl Pts',(-19.6025755757097,-20.8826312758761,
6.16679084379954));
#162131=CARTESIAN_POINT('Ctrl Pts',(-19.5948490539073,-20.8860888183434,
6.16628016013403));
#162132=CARTESIAN_POINT('Ctrl Pts',(-19.5668348071423,-20.8984237932242,
6.16442766854472));
#162133=CARTESIAN_POINT('Ctrl Pts',(-19.5464293832845,-20.9070288584913,
6.16307661912572));
#162134=CARTESIAN_POINT('Ctrl Pts',(-19.3541095852768,-20.984600208948,
6.15032301682864));
#162135=CARTESIAN_POINT('Ctrl Pts',(-19.1740053997905,-21.031030376741,
6.13812470538277));
#162136=CARTESIAN_POINT('Ctrl Pts',(-18.9104071992707,-21.0631685341847,
6.12059190829744));
#162137=CARTESIAN_POINT('Ctrl Pts',(-18.8301098525211,-21.0683451279764,
6.11530922327973));
#162138=CARTESIAN_POINT('Ctrl Pts',(-18.7136130670479,-21.0692095534174,
6.1078823534815));
#162139=CARTESIAN_POINT('Ctrl Pts',(-18.6775145577286,-21.0685541984524,
6.10561444227034));
#162140=CARTESIAN_POINT('Ctrl Pts',(-18.633984969242,-21.0666493323093,
6.10293381883117));
#162141=CARTESIAN_POINT('Ctrl Pts',(-18.6265234886838,-21.0662832374951,
6.10247625427274));
#162142=CARTESIAN_POINT('Ctrl Pts',(-18.614909936501,-21.0656517839587,
6.1017672327431));
#162143=CARTESIAN_POINT('Ctrl Pts',(-18.6107565307587,-21.0654136734281,
6.1015142924468));
#162144=CARTESIAN_POINT('Ctrl Pts',(-18.6030445165533,-21.0649487395556,
6.1010458393058));
#162145=CARTESIAN_POINT('Ctrl Pts',(-18.5994858128871,-21.0647251710473,
6.10083015236547));
#162146=CARTESIAN_POINT('Ctrl Pts',(-18.5914280222152,-21.0641985143231,
6.10034285816504));
#162147=CARTESIAN_POINT('Ctrl Pts',(-18.5869293402096,-21.06389004322,6.10007155579034));
#162148=CARTESIAN_POINT('Ctrl Pts',(-18.575318338226,-21.0630566050789,
6.09937320108826));
#162149=CARTESIAN_POINT('Ctrl Pts',(-18.5682075575847,-21.0625100636874,
6.09894732958605));
#162150=CARTESIAN_POINT('Ctrl Pts',(-18.5245995980859,-21.0589365593799,
6.09634599517287));
#162151=CARTESIAN_POINT('Ctrl Pts',(-18.4881808926155,-21.0549986976973,
6.09421816496268));
#162152=CARTESIAN_POINT('Ctrl Pts',(-18.2828037996395,-21.0273830302017,
6.08238008614659));
#162153=CARTESIAN_POINT('Ctrl Pts',(-18.1170802547153,-20.9842930045862,
6.0734041916488));
#162154=CARTESIAN_POINT('Ctrl Pts',(-17.8695853032667,-20.8868306854097,
6.05877220236035));
#162155=CARTESIAN_POINT('Ctrl Pts',(-17.7833289432465,-20.8459387582868,
6.05342533555794));
#162156=CARTESIAN_POINT('Ctrl Pts',(-17.6814645164485,-20.7889309953434,
6.04662804272619));
#162157=CARTESIAN_POINT('Ctrl Pts',(-17.6629608295743,-20.7782041156094,
6.04537307950603));
#162158=CARTESIAN_POINT('Ctrl Pts',(-17.6368985461135,-20.7625630517011,
6.04357508507643));
#162159=CARTESIAN_POINT('Ctrl Pts',(-17.6292035343362,-20.757877883452,
6.04304039277113));
#162160=CARTESIAN_POINT('Ctrl Pts',(-17.6159861778431,-20.7497142948798,
6.04211524976306));
#162161=CARTESIAN_POINT('Ctrl Pts',(-17.6104495410475,-20.7462591666941,
6.04172566005054));
#162162=CARTESIAN_POINT('Ctrl Pts',(-17.5998832179371,-20.7395971877396,
6.04097816807181));
#162163=CARTESIAN_POINT('Ctrl Pts',(-17.5948509283285,-20.7363945674513,
6.04062042530392));
#162164=CARTESIAN_POINT('Ctrl Pts',(-17.5818091895734,-20.7280169672079,
6.03968871343354));
#162165=CARTESIAN_POINT('Ctrl Pts',(-17.5738211167267,-20.7228091047865,
6.03911352070479));
#162166=CARTESIAN_POINT('Ctrl Pts',(-17.5467468687812,-20.7048960898247,
6.03714837701873));
#162167=CARTESIAN_POINT('Ctrl Pts',(-17.5278325493053,-20.6919352618201,
6.03574883757156));
#162168=CARTESIAN_POINT('Ctrl Pts',(-17.3652842988574,-20.5766266259218,
6.02348271163937));
#162169=CARTESIAN_POINT('Ctrl Pts',(-17.2347769488205,-20.4570251849565,
6.01190444970991));
#162170=CARTESIAN_POINT('Ctrl Pts',(-17.0646907389936,-20.2568219800019,
5.99454841312577));
#162171=CARTESIAN_POINT('Ctrl Pts',(-17.0128306891587,-20.1876099355561,
5.98885571168467));
#162172=CARTESIAN_POINT('Ctrl Pts',(-16.9446426697063,-20.0839488401,5.98093496450927));
#162173=CARTESIAN_POINT('Ctrl Pts',(-16.9247842413231,-20.0519302596216,
5.97856583002893));
#162174=CARTESIAN_POINT('Ctrl Pts',(-16.9019763393875,-20.0128654501939,
5.97578227494572));
#162175=CARTESIAN_POINT('Ctrl Pts',(-16.8981980989368,-20.0063137960191,
5.97531897400177));
#162176=CARTESIAN_POINT('Ctrl Pts',(-16.8923860703478,-19.996109481399,
5.97460301792126));
#162177=CARTESIAN_POINT('Ctrl Pts',(-16.8903278990199,-19.9924708836874,
5.97434883320603));
#162178=CARTESIAN_POINT('Ctrl Pts',(-16.8865350407324,-19.9857189780537,
5.97387924108417));
#162179=CARTESIAN_POINT('Ctrl Pts',(-16.8847974526987,-19.9826074134515,
5.97366365223436));
#162180=CARTESIAN_POINT('Ctrl Pts',(-16.8808921200445,-19.9755723118657,
5.97317805058498));
#162181=CARTESIAN_POINT('Ctrl Pts',(-16.8787289803507,-19.971646280271,
5.97290833364313));
#162182=CARTESIAN_POINT('Ctrl Pts',(-16.8723961207589,-19.96006546309,5.9721164086354));
#162183=CARTESIAN_POINT('Ctrl Pts',(-16.8682611313399,-19.9523916537852,
5.97159636300104));
#162184=CARTESIAN_POINT('Ctrl Pts',(-16.8391843743181,-19.8976229359669,
5.96791656424516));
#162185=CARTESIAN_POINT('Ctrl Pts',(-16.8159791199815,-19.8496223666053,
5.9648579862251));
#162186=CARTESIAN_POINT('Ctrl Pts',(-16.7878680592657,-19.7853919224357,
5.96091481108591));
#162187=CARTESIAN_POINT('Ctrl Pts',(-16.7813111923146,-19.7699107949034,
5.959975541821));
#162188=CARTESIAN_POINT('Ctrl Pts',(-16.7185516531651,-19.6166743055174,
5.95077269045208));
#162189=CARTESIAN_POINT('Ctrl Pts',(-16.6768332173567,-19.4734329147004,
5.94288593558575));
#162190=CARTESIAN_POINT('Ctrl Pts',(-16.6395602777455,-19.266339899341,
5.93124378932298));
#162191=CARTESIAN_POINT('Ctrl Pts',(-16.6312979563321,-19.2052401723438,
5.9277849957254));
#162192=CARTESIAN_POINT('Ctrl Pts',(-16.6223429019767,-19.1068412132478,
5.92211439282943));
#162193=CARTESIAN_POINT('Ctrl Pts',(-16.6199492677345,-19.0697317040826,
5.91995341939017));
#162194=CARTESIAN_POINT('Ctrl Pts',(-16.6181106058018,-19.0214613240935,
5.91710590560176));
#162195=CARTESIAN_POINT('Ctrl Pts',(-16.6177747565675,-19.0103396600716,
5.91644732130659));
#162196=CARTESIAN_POINT('Ctrl Pts',(-16.6173711879845,-18.9922495687759,
5.9153718212583));
#162197=CARTESIAN_POINT('Ctrl Pts',(-16.6172501725339,-18.9852824545151,
5.91495657978525));
#162198=CARTESIAN_POINT('Ctrl Pts',(-16.6170836125737,-18.9718839711603,
5.91415599775826));
#162199=CARTESIAN_POINT('Ctrl Pts',(-16.6170329747036,-18.9654527341202,
5.91377082141));
#162200=CARTESIAN_POINT('Ctrl Pts',(-16.6169841377968,-18.9507281979257,
5.9128868464682));
#162201=CARTESIAN_POINT('Ctrl Pts',(-16.617005364764,-18.9424349790369,
5.91238744439236));
#162202=CARTESIAN_POINT('Ctrl Pts',(-16.6171911963953,-18.9204058743269,
5.91105674736304));
#162203=CARTESIAN_POINT('Ctrl Pts',(-16.6174407656691,-18.9066712739723,
5.91022280649256));
#162204=CARTESIAN_POINT('Ctrl Pts',(-16.6203575480668,-18.8021596104344,
5.90384346646464));
#162205=CARTESIAN_POINT('Ctrl Pts',(-16.6287295390135,-18.7116480599021,
5.89811957756085));
#162206=CARTESIAN_POINT('Ctrl Pts',(-16.6647945271128,-18.483140163643,
5.88317960886447));
#162207=CARTESIAN_POINT('Ctrl Pts',(-16.7004741667683,-18.3468482943189,
5.87378633691796));
#162208=CARTESIAN_POINT('Ctrl Pts',(-16.7682319149218,-18.1643607000658,
5.86104500790171));
#162209=CARTESIAN_POINT('Ctrl Pts',(-16.7890172317557,-18.1143469324901,
5.85753903952122));
#162210=CARTESIAN_POINT('Ctrl Pts',(-16.8234640977505,-18.039678553686,
5.85233645326813));
#162211=CARTESIAN_POINT('Ctrl Pts',(-16.8357367009845,-18.0144102813451,
5.85058167652124));
#162212=CARTESIAN_POINT('Ctrl Pts',(-16.8516520833486,-17.9832363056716,
5.84843086234387));
#162213=CARTESIAN_POINT('Ctrl Pts',(-16.8548251434399,-17.9770955758191,
5.84800788227506));
#162214=CARTESIAN_POINT('Ctrl Pts',(-16.8598991621421,-17.9673927945477,
5.84734077684181));
#162215=CARTESIAN_POINT('Ctrl Pts',(-16.8617803004878,-17.9638205138352,
5.84709543424074));
#162216=CARTESIAN_POINT('Ctrl Pts',(-16.8653510635632,-17.9570864340622,
5.84663347558478));
#162217=CARTESIAN_POINT('Ctrl Pts',(-16.8670384790357,-17.9539235847165,
5.84641673142875));
#162218=CARTESIAN_POINT('Ctrl Pts',(-16.8709195724475,-17.9466932426711,
5.8459217497663));
#162219=CARTESIAN_POINT('Ctrl Pts',(-16.8731185379313,-17.9426286407291,
5.84564385212606));
#162220=CARTESIAN_POINT('Ctrl Pts',(-16.8790018237925,-17.9318384575283,
5.84490699899004));
#162221=CARTESIAN_POINT('Ctrl Pts',(-16.8827094469492,-17.9251255682,5.84444948741176));
#162222=CARTESIAN_POINT('Ctrl Pts',(-16.909220316352,-17.8777362295717,
5.84122508016357));
#162223=CARTESIAN_POINT('Ctrl Pts',(-16.9333274430777,-17.8377995728001,
5.83853584201645));
#162224=CARTESIAN_POINT('Ctrl Pts',(-16.9612096157079,-17.7948812206126,
5.83564063338084));
#162225=CARTESIAN_POINT('Ctrl Pts',(-16.9636954794544,-17.7910816043858,
5.83538427195669));
#162226=CARTESIAN_POINT('Ctrl Pts',(-16.9790311182565,-17.7678050455661,
5.83381333308899));
#162227=CARTESIAN_POINT('Ctrl Pts',(-16.9921902791466,-17.7485331670506,
5.83251067145313));
#162228=CARTESIAN_POINT('Ctrl Pts',(-17.0319419082789,-17.6923343035576,
5.82869415952251));
#162229=CARTESIAN_POINT('Ctrl Pts',(-17.0594097316307,-17.6560420220676,
5.82620612657616));
#162230=CARTESIAN_POINT('Ctrl Pts',(-17.1567932640125,-17.5356437880277,
5.81777532092394));
#162231=CARTESIAN_POINT('Ctrl Pts',(-17.2320431804647,-17.4560819422162,
5.81188731274403));
#162232=CARTESIAN_POINT('Ctrl Pts',(-17.3539496719778,-17.3457039537544,
5.80274316712434));
#162233=CARTESIAN_POINT('Ctrl Pts',(-17.3962268068528,-17.3103276409578,
5.79963575995488));
#162234=CARTESIAN_POINT('Ctrl Pts',(-17.4669834836391,-17.2556701091351,
5.79449191356694));
#162235=CARTESIAN_POINT('Ctrl Pts',(-17.4946377919628,-17.2353616944497,
5.79249485870071));
#162236=CARTESIAN_POINT('Ctrl Pts',(-17.5316371066315,-17.2095507746281,
5.78983427677929));
#162237=CARTESIAN_POINT('Ctrl Pts',(-17.5405490939458,-17.203434657032,
5.78919427657986));
#162238=CARTESIAN_POINT('Ctrl Pts',(-17.5552247326988,-17.1935275226246,
5.78814157730774));
#162239=CARTESIAN_POINT('Ctrl Pts',(-17.5609608388292,-17.1896959090112,
5.78773041947644));
#162240=CARTESIAN_POINT('Ctrl Pts',(-17.5721021388198,-17.182332220164,
5.78693235184349));
#162241=CARTESIAN_POINT('Ctrl Pts',(-17.5775049727688,-17.1787967004989,
5.78654557740911));
#162242=CARTESIAN_POINT('Ctrl Pts',(-17.5900196131293,-17.1706888655283,
5.78565019378876));
#162243=CARTESIAN_POINT('Ctrl Pts',(-17.5971427698195,-17.1661343504382,
5.78514092845027));
#162244=CARTESIAN_POINT('Ctrl Pts',(-17.6163783350559,-17.1539969347018,
5.78376659877236));
#162245=CARTESIAN_POINT('Ctrl Pts',(-17.6285403945448,-17.1464939064731,
5.78289860622476));
#162246=CARTESIAN_POINT('Ctrl Pts',(-17.7408543942565,-17.0787652857835,
5.77489029412853));
#162247=CARTESIAN_POINT('Ctrl Pts',(-17.8457402330073,-17.0268160438482,
5.76744810588576));
#162248=CARTESIAN_POINT('Ctrl Pts',(-18.1056911581054,-16.9238453656543,
5.74918452634749));
#162249=CARTESIAN_POINT('Ctrl Pts',(-18.2634257144639,-16.8815548440293,
5.73822295915745));
#162250=CARTESIAN_POINT('Ctrl Pts',(-18.4565509253096,-16.8530087668865,
5.72581866731969));
#162251=CARTESIAN_POINT('Ctrl Pts',(-18.4887619029087,-16.8490019665329,
5.72378474652386));
#162252=CARTESIAN_POINT('Ctrl Pts',(-18.5282533819443,-16.8450093292195,
5.72134394612462));
#162253=CARTESIAN_POINT('Ctrl Pts',(-18.5354563422,-16.844318388127,5.72090090583395));
#162254=CARTESIAN_POINT('Ctrl Pts',(-18.5467548495372,-16.8432930179311,
5.72020946638671));
#162255=CARTESIAN_POINT('Ctrl Pts',(-18.5508479896444,-16.8429335656827,
5.7199596983162));
#162256=CARTESIAN_POINT('Ctrl Pts',(-18.5585013941033,-16.8422839057024,
5.71949406034148));
#162257=CARTESIAN_POINT('Ctrl Pts',(-18.5620613071291,-16.8419907949648,
5.71927803528614));
#162258=CARTESIAN_POINT('Ctrl Pts',(-18.5701900930888,-16.8413422081078,
5.7187860253456));
#162259=CARTESIAN_POINT('Ctrl Pts',(-18.5747593802421,-16.8409925566207,
5.71851037005742));
#162260=CARTESIAN_POINT('Ctrl Pts',(-18.5888102378123,-16.8399632357146,
5.71766540856972));
#162261=CARTESIAN_POINT('Ctrl Pts',(-18.5982954299812,-16.8393325775135,
5.71709878076436));
#162262=CARTESIAN_POINT('Ctrl Pts',(-18.683689920298,-16.8342322969739,
5.71202884219081));
#162263=CARTESIAN_POINT('Ctrl Pts',(-18.7597932037826,-16.8337912103267,
5.70773273720709));
#162264=CARTESIAN_POINT('Ctrl Pts',(-18.8781845333406,-16.8394887975101,
5.70117313781305));
#162265=CARTESIAN_POINT('Ctrl Pts',(-18.9205362033227,-16.8428065078548,
5.69885152820335));
#162266=CARTESIAN_POINT('Ctrl Pts',(-19.0714391837038,-16.8592089376823,
5.69058749971214));
#162267=CARTESIAN_POINT('Ctrl Pts',(-19.179038682833,-16.8794220601524,
5.68470091809202));
#162268=CARTESIAN_POINT('Ctrl Pts',(-19.3377693555559,-16.9221762172933,
5.67556008892389));
#162269=CARTESIAN_POINT('Ctrl Pts',(-19.3903645927526,-16.9385683769579,
5.67245458262747));
#162270=CARTESIAN_POINT('Ctrl Pts',(-19.4745732409515,-16.9684637297445,
5.66731360235643));
#162271=CARTESIAN_POINT('Ctrl Pts',(-19.5066030971589,-16.9807189143662,
5.66531745520338));
#162272=CARTESIAN_POINT('Ctrl Pts',(-19.5483165361838,-16.9978520092493,
5.66265791123408));
#162273=CARTESIAN_POINT('Ctrl Pts',(-19.5582814113878,-17.0020343748818,
5.66201801784993));
#162274=CARTESIAN_POINT('Ctrl Pts',(-19.5745533217416,-17.0090108872502,
5.66096544951941));
#162275=CARTESIAN_POINT('Ctrl Pts',(-19.5808795733104,-17.0117599206456,
5.66055431506169));
#162276=CARTESIAN_POINT('Ctrl Pts',(-19.5931016142093,-17.0171420958222,
5.65975626080593));
#162277=CARTESIAN_POINT('Ctrl Pts',(-19.5989990202117,-17.0197713938314,
5.65936947620586));
#162278=CARTESIAN_POINT('Ctrl Pts',(-19.6125913967767,-17.0259061140363,
5.65847402243893));
#162279=CARTESIAN_POINT('Ctrl Pts',(-19.6202775395163,-17.0294307243313,
5.65796469679604));
#162280=CARTESIAN_POINT('Ctrl Pts',(-19.6408989791659,-17.0390369716712,
5.65659009885363));
#162281=CARTESIAN_POINT('Ctrl Pts',(-19.6537939662945,-17.0452036422302,
5.65572189656714));
#162282=CARTESIAN_POINT('Ctrl Pts',(-19.7717737099056,-17.1030994109468,
5.64769737814423));
#162283=CARTESIAN_POINT('Ctrl Pts',(-19.8724413164911,-17.1633269806716,
5.64023777418421));
#162284=CARTESIAN_POINT('Ctrl Pts',(-20.1005659073467,-17.3268981327463,
5.62190029248212));
#162285=CARTESIAN_POINT('Ctrl Pts',(-20.2220276625825,-17.4373276444542,
5.61088001980022));
#162286=CARTESIAN_POINT('Ctrl Pts',(-20.3502424711645,-17.584359854051,
5.59849619923141));
#162287=CARTESIAN_POINT('Ctrl Pts',(-20.3703947342259,-17.6085373792621,
5.59652530378752));
#162288=CARTESIAN_POINT('Ctrl Pts',(-20.3944666603229,-17.6387632201585,
5.59414958451253));
#162289=CARTESIAN_POINT('Ctrl Pts',(-20.3989032904284,-17.644392487449,
5.59371079159916));
#162290=CARTESIAN_POINT('Ctrl Pts',(-20.4058289752123,-17.6532723008965,
5.5930244998631));
#162291=CARTESIAN_POINT('Ctrl Pts',(-20.4083372881398,-17.6565076592358,
5.59277566485376));
#162292=CARTESIAN_POINT('Ctrl Pts',(-20.4130180235565,-17.6625814286736,
5.59231082845444));
#162293=CARTESIAN_POINT('Ctrl Pts',(-20.415192617805,-17.6654180330958,
5.59209467755134));
#162294=CARTESIAN_POINT('Ctrl Pts',(-20.4201529741126,-17.6719225176489,
5.59160116008826));
#162295=CARTESIAN_POINT('Ctrl Pts',(-20.4229339523977,-17.6755939837619,
5.59132413091035));
#162296=CARTESIAN_POINT('Ctrl Pts',(-20.4301820178,-17.6852280910533,5.5906011224146));
#162297=CARTESIAN_POINT('Ctrl Pts',(-20.4346296941597,-17.6912053482633,
5.59015646706207));
#162298=CARTESIAN_POINT('Ctrl Pts',(-20.4640847896414,-17.7312296782737,
5.58720412581317));
#162299=CARTESIAN_POINT('Ctrl Pts',(-20.4881017004804,-17.7659977568095,
5.58476004801791));
#162300=CARTESIAN_POINT('Ctrl Pts',(-20.5515194671736,-17.8639498378017,
5.57813166305266));
#162301=CARTESIAN_POINT('Ctrl Pts',(-20.5886541327809,-17.9285305558673,
5.5740439278453));
#162302=CARTESIAN_POINT('Ctrl Pts',(-20.6602986497802,-18.0698871727679,
5.56540875113171));
#162303=CARTESIAN_POINT('Ctrl Pts',(-20.6937779253687,-18.1470084993638,
5.5608776423495));
#162304=CARTESIAN_POINT('Ctrl Pts',(-20.7225805962997,-18.2258896695266,
5.55626859415409));
#162305=CARTESIAN_POINT('',(-20.8509995343428,-18.9505958660381,6.0890562790225));
#162306=CARTESIAN_POINT('Ctrl Pts',(-20.7225805585332,-18.2258895660964,
5.33540095489714));
#162307=CARTESIAN_POINT('Ctrl Pts',(-20.7135660112331,-18.2012016499504,
5.33706792095253));
#162308=CARTESIAN_POINT('Ctrl Pts',(-20.7040899377832,-18.1766767254248,
5.33871643378043));
#162309=CARTESIAN_POINT('Ctrl Pts',(-20.6904971171894,-18.143358003269,
5.34093970850242));
#162310=CARTESIAN_POINT('Ctrl Pts',(-20.6867761540128,-18.1344132162557,
5.34153493717554));
#162311=CARTESIAN_POINT('Ctrl Pts',(-20.6811908866969,-18.1212425280375,
5.34240861895589));
#162312=CARTESIAN_POINT('Ctrl Pts',(-20.6793740068711,-18.1169968258862,
5.34268983322622));
#162313=CARTESIAN_POINT('Ctrl Pts',(-20.676125788991,-18.1094745083999,
5.34318727343144));
#162314=CARTESIAN_POINT('Ctrl Pts',(-20.6747000298907,-18.1061955433311,
5.34340383377577));
#162315=CARTESIAN_POINT('Ctrl Pts',(-20.6716271661213,-18.0991772400302,
5.34386676465063));
#162316=CARTESIAN_POINT('Ctrl Pts',(-20.6699775458628,-18.0954390638267,
5.34411297866601));
#162317=CARTESIAN_POINT('Ctrl Pts',(-20.6654189078965,-18.0851892564606,
5.34478715773716));
#162318=CARTESIAN_POINT('Ctrl Pts',(-20.6624877611379,-18.0786874435046,
5.34521378895089));
#162319=CARTESIAN_POINT('Ctrl Pts',(-20.6466515921782,-18.0440285031547,
5.34748317357265));
#162320=CARTESIAN_POINT('Ctrl Pts',(-20.6331619274932,-18.0161407406079,
5.34929208090094));
#162321=CARTESIAN_POINT('Ctrl Pts',(-20.5446480403026,-17.842955145594,
5.36047872978793));
#162322=CARTESIAN_POINT('Ctrl Pts',(-20.4536052723327,-17.7064491710487,
5.36912124662805));
#162323=CARTESIAN_POINT('Ctrl Pts',(-20.2715338980583,-17.4920196635696,
5.38451638569335));
#162324=CARTESIAN_POINT('Ctrl Pts',(-20.18797841007,-17.4087908422596,5.39108663600945));
#162325=CARTESIAN_POINT('Ctrl Pts',(-20.0870076680023,-17.3237298193577,
5.39882095723859));
#162326=CARTESIAN_POINT('Ctrl Pts',(-20.0759772265521,-17.3146269089445,
5.39966313469165));
#162327=CARTESIAN_POINT('Ctrl Pts',(-20.058277884116,-17.300319454549,5.40101058571771));
#162328=CARTESIAN_POINT('Ctrl Pts',(-20.0516684377585,-17.2950418159929,
5.40151291206349));
#162329=CARTESIAN_POINT('Ctrl Pts',(-20.0399575021166,-17.2858050232956,
5.40240155250734));
#162330=CARTESIAN_POINT('Ctrl Pts',(-20.034869163559,-17.2818293154277,
5.40278719948083));
#162331=CARTESIAN_POINT('Ctrl Pts',(-20.024308750341,-17.2736556089414,
5.40358666493282));
#162332=CARTESIAN_POINT('Ctrl Pts',(-20.0188341972768,-17.2694609514304,
5.40400060920177));
#162333=CARTESIAN_POINT('Ctrl Pts',(-20.0047322515299,-17.2587648583807,
5.40506566588964));
#162334=CARTESIAN_POINT('Ctrl Pts',(-19.9960754930004,-17.2523026319117,
5.4057183052982));
#162335=CARTESIAN_POINT('Ctrl Pts',(-19.9597641850371,-17.2256267725265,
5.40845129989368));
#162336=CARTESIAN_POINT('Ctrl Pts',(-19.9316718048834,-17.2060205069075,
5.41055492107091));
#162337=CARTESIAN_POINT('Ctrl Pts',(-19.8572712356199,-17.156735416053,
5.41610187652821));
#162338=CARTESIAN_POINT('Ctrl Pts',(-19.8102625662508,-17.1281657785285,
5.41958346675837));
#162339=CARTESIAN_POINT('Ctrl Pts',(-19.666653594967,-17.0483736690716,
5.43014244420328));
#162340=CARTESIAN_POINT('Ctrl Pts',(-19.5671477062197,-17.0027700578779,
5.43736825701715));
#162341=CARTESIAN_POINT('Ctrl Pts',(-19.4286084545432,-16.951830855491,
5.44711898869856));
#162342=CARTESIAN_POINT('Ctrl Pts',(-19.3922884268291,-16.9395850430519,
5.44964658586146));
#162343=CARTESIAN_POINT('Ctrl Pts',(-19.3246467361848,-16.918806031766,
5.45428250504768));
#162344=CARTESIAN_POINT('Ctrl Pts',(-19.2934220655813,-16.909994031609,
5.45639500985962));
#162345=CARTESIAN_POINT('Ctrl Pts',(-19.256085492626,-16.9003779298283,
5.45887994061256));
#162346=CARTESIAN_POINT('Ctrl Pts',(-19.2501581272849,-16.8988786764193,
5.45927321318656));
#162347=CARTESIAN_POINT('Ctrl Pts',(-19.2018755185495,-16.886888497545,
5.46246634254817));
#162348=CARTESIAN_POINT('Ctrl Pts',(-19.1592082255338,-16.8776828625035,
5.46522351884134));
#162349=CARTESIAN_POINT('Ctrl Pts',(-19.1088857525218,-16.8684438459875,
5.46837679874758));
#162350=CARTESIAN_POINT('Ctrl Pts',(-19.1014804961831,-16.8671250245751,
5.4688383358078));
#162351=CARTESIAN_POINT('Ctrl Pts',(-19.0895084869368,-16.8650586672177,
5.46958031171733));
#162352=CARTESIAN_POINT('Ctrl Pts',(-19.0849461127333,-16.8642866006908,
5.46986208886646));
#162353=CARTESIAN_POINT('Ctrl Pts',(-19.0768529212297,-16.862944312483,
5.47036015182437));
#162354=CARTESIAN_POINT('Ctrl Pts',(-19.0733231563496,-16.8623680737048,
5.47057677515913));
#162355=CARTESIAN_POINT('Ctrl Pts',(-19.0657633011453,-16.8611535780393,
5.47103942893412));
#162356=CARTESIAN_POINT('Ctrl Pts',(-19.0617328320122,-16.8605180278854,
5.47128530500882));
#162357=CARTESIAN_POINT('Ctrl Pts',(-19.0506781036699,-16.8588075880518,
5.47195760577381));
#162358=CARTESIAN_POINT('Ctrl Pts',(-19.0436501562667,-16.8577563945981,
5.47238270898023));
#162359=CARTESIAN_POINT('Ctrl Pts',(-19.0063137545842,-16.8523639226998,
5.47462949566018));
#162360=CARTESIAN_POINT('Ctrl Pts',(-18.9759173890594,-16.8486449097502,
5.47641812652884));
#162361=CARTESIAN_POINT('Ctrl Pts',(-18.8840169356094,-16.8394196148042,
5.48173263747361));
#162362=CARTESIAN_POINT('Ctrl Pts',(-18.8223395391613,-16.8359427705003,
5.48517443335155));
#162363=CARTESIAN_POINT('Ctrl Pts',(-18.6140799929785,-16.8333263510387,
5.49662776081094));
#162364=CARTESIAN_POINT('Ctrl Pts',(-18.4677734657393,-16.8467011993875,
5.504421425657));
#162365=CARTESIAN_POINT('Ctrl Pts',(-18.2500273164865,-16.8896839391248,
5.51680892369875));
#162366=CARTESIAN_POINT('Ctrl Pts',(-18.1768760839219,-16.9082318526576,
5.52110478521814));
#162367=CARTESIAN_POINT('Ctrl Pts',(-18.0923220510918,-16.9345483256142,
5.52630057373922));
#162368=CARTESIAN_POINT('Ctrl Pts',(-18.0798057078927,-16.9385721604367,
5.52707566604996));
#162369=CARTESIAN_POINT('Ctrl Pts',(-18.0595388562537,-16.9452966056,5.52834078923163));
#162370=CARTESIAN_POINT('Ctrl Pts',(-18.0517650280505,-16.9479262020394,
5.52882847957221));
#162371=CARTESIAN_POINT('Ctrl Pts',(-18.0379553303796,-16.952687170475,
5.52969922967628));
#162372=CARTESIAN_POINT('Ctrl Pts',(-18.0319134375454,-16.9548008537353,
5.53008169916945));
#162373=CARTESIAN_POINT('Ctrl Pts',(-18.0192089621152,-16.9593101343908,
5.53088914843016));
#162374=CARTESIAN_POINT('Ctrl Pts',(-18.0125486365597,-16.9617118156818,
5.53131432693003));
#162375=CARTESIAN_POINT('Ctrl Pts',(-17.9949779392209,-16.968147509922,
5.53244101641201));
#162376=CARTESIAN_POINT('Ctrl Pts',(-17.9840886665018,-16.9722380718542,
5.53314440929393));
#162377=CARTESIAN_POINT('Ctrl Pts',(-17.9338102135396,-16.9915995300672,
5.53641641630369));
#162378=CARTESIAN_POINT('Ctrl Pts',(-17.8948522858883,-17.007956685442,
5.53902131813492));
#162379=CARTESIAN_POINT('Ctrl Pts',(-17.7890749204608,-17.0561411626773,
5.54629293078017));
#162380=CARTESIAN_POINT('Ctrl Pts',(-17.7233988435647,-17.0903212964203,
5.55103442014254));
#162381=CARTESIAN_POINT('Ctrl Pts',(-17.528073950343,-17.2053605156642,
5.5657968061218));
#162382=CARTESIAN_POINT('Ctrl Pts',(-17.405273586751,-17.2968591907233,
5.57605686761176));
#162383=CARTESIAN_POINT('Ctrl Pts',(-17.2580948998451,-17.4335426444481,
5.58899242826385));
#162384=CARTESIAN_POINT('Ctrl Pts',(-17.2239295827149,-17.46751465858,5.59204440728228));
#162385=CARTESIAN_POINT('Ctrl Pts',(-17.1856498353416,-17.508268478083,
5.59549198810629));
#162386=CARTESIAN_POINT('Ctrl Pts',(-17.1803802319196,-17.5139406965637,
5.59596722427078));
#162387=CARTESIAN_POINT('Ctrl Pts',(-17.1720004384982,-17.5230605590853,
5.59672379565999));
#162388=CARTESIAN_POINT('Ctrl Pts',(-17.1688703244286,-17.5264896859279,
5.59700658960716));
#162389=CARTESIAN_POINT('Ctrl Pts',(-17.1633415316753,-17.5325867948411,
5.59750638975362));
#162390=CARTESIAN_POINT('Ctrl Pts',(-17.1609383238777,-17.535250609689,
5.59772373654553));
#162391=CARTESIAN_POINT('Ctrl Pts',(-17.1558533954762,-17.5409158444572,
5.59818381408242));
#162392=CARTESIAN_POINT('Ctrl Pts',(-17.1531734648347,-17.5439188000216,
5.59842641171024));
#162393=CARTESIAN_POINT('Ctrl Pts',(-17.1459516885744,-17.5520576563149,
5.599080541687));
#162394=CARTESIAN_POINT('Ctrl Pts',(-17.1414261561243,-17.5572080585964,
5.59949086952868));
#162395=CARTESIAN_POINT('Ctrl Pts',(-17.1189400086327,-17.5830511383967,
5.60153230711408));
#162396=CARTESIAN_POINT('Ctrl Pts',(-17.1013563914851,-17.604070190905,
5.60313711806937));
#162397=CARTESIAN_POINT('Ctrl Pts',(-17.0514933329909,-17.6660831771208,
5.60773291477103));
#162398=CARTESIAN_POINT('Ctrl Pts',(-17.0203135728354,-17.7079379729551,
5.6106643157784));
#162399=CARTESIAN_POINT('Ctrl Pts',(-16.9116076690405,-17.865715536876,
5.62127357467201));
#162400=CARTESIAN_POINT('Ctrl Pts',(-16.8440392596118,-17.9880609395962,
5.62868690682174));
#162401=CARTESIAN_POINT('Ctrl Pts',(-16.751676510829,-18.2029915233819,
5.64161059620066));
#162402=CARTESIAN_POINT('Ctrl Pts',(-16.7202241469305,-18.2922093393727,
5.6469441738315));
#162403=CARTESIAN_POINT('Ctrl Pts',(-16.6911214235892,-18.3965474969471,
5.65329380954537));
#162404=CARTESIAN_POINT('Ctrl Pts',(-16.6875355641712,-18.4099080701129,
5.65410879298426));
#162405=CARTESIAN_POINT('Ctrl Pts',(-16.6820027344617,-18.4313605168971,
5.65542081972188));
#162406=CARTESIAN_POINT('Ctrl Pts',(-16.6799720577307,-18.4394305329991,
5.65591515598409));
#162407=CARTESIAN_POINT('Ctrl Pts',(-16.6764553774996,-18.4537625613928,
5.65679453493138));
#162408=CARTESIAN_POINT('Ctrl Pts',(-16.6749502422923,-18.4600198045835,
5.65717895512081));
#162409=CARTESIAN_POINT('Ctrl Pts',(-16.6718778942383,-18.4730534516674,
5.65798075132927));
#162410=CARTESIAN_POINT('Ctrl Pts',(-16.6703154998704,-18.4798309017319,
5.65839827728063));
#162411=CARTESIAN_POINT('Ctrl Pts',(-16.6663534353189,-18.4974131706843,
5.6594830328968));
#162412=CARTESIAN_POINT('Ctrl Pts',(-16.6640050737539,-18.5082292260038,
5.66015189999645));
#162413=CARTESIAN_POINT('Ctrl Pts',(-16.6542496807475,-18.5549235402367,
5.66304652316464));
#162414=CARTESIAN_POINT('Ctrl Pts',(-16.6476901973596,-18.590970569524,
5.6652991249978));
#162415=CARTESIAN_POINT('Ctrl Pts',(-16.6328073443966,-18.6868166955601,
5.67133982202806));
#162416=CARTESIAN_POINT('Ctrl Pts',(-16.6261013401342,-18.7468294803527,
5.67517521063258));
#162417=CARTESIAN_POINT('Ctrl Pts',(-16.6106548534774,-18.9718850524776,
5.68973439322023));
#162418=CARTESIAN_POINT('Ctrl Pts',(-16.6186785147509,-19.1374675704465,
5.70085095367274));
#162419=CARTESIAN_POINT('Ctrl Pts',(-16.6466295126158,-19.3049798581185,
5.71184199648554));
#162420=CARTESIAN_POINT('Ctrl Pts',(-16.6474045776612,-19.3095330415694,
5.71214050335372));
#162421=CARTESIAN_POINT('Ctrl Pts',(-16.6483125256036,-19.3147633319331,
5.7124830972345));
#162422=CARTESIAN_POINT('Ctrl Pts',(-16.6484308417836,-19.3154429283221,
5.7125276061728));
#162423=CARTESIAN_POINT('Ctrl Pts',(-16.6504318302204,-19.3269032548044,
5.71327807870787));
#162424=CARTESIAN_POINT('Ctrl Pts',(-16.6523977688055,-19.3376694531432,
5.71398159220466));
#162425=CARTESIAN_POINT('Ctrl Pts',(-16.6620277805191,-19.3881868693206,
5.71727416243951));
#162426=CARTESIAN_POINT('Ctrl Pts',(-16.6707481340064,-19.4277311132873,
5.71982693886713));
#162427=CARTESIAN_POINT('Ctrl Pts',(-16.6823874262688,-19.4741388318139,
5.72277464005917));
#162428=CARTESIAN_POINT('Ctrl Pts',(-16.6842141588694,-19.4812646988971,
5.72322589934859));
#162429=CARTESIAN_POINT('Ctrl Pts',(-16.6872377838357,-19.4928090075172,
5.72395459646749));
#162430=CARTESIAN_POINT('Ctrl Pts',(-16.6884119106158,-19.4972332726534,
5.72423329782207));
#162431=CARTESIAN_POINT('Ctrl Pts',(-16.6905276796529,-19.5051027312929,
5.72472797305055));
#162432=CARTESIAN_POINT('Ctrl Pts',(-16.6914636975086,-19.5085493770067,
5.72494426740744));
#162433=CARTESIAN_POINT('Ctrl Pts',(-16.693496256492,-19.5159595587861,
5.72540850548611));
#162434=CARTESIAN_POINT('Ctrl Pts',(-16.694595622108,-19.519922261681,5.72565628283512));
#162435=CARTESIAN_POINT('Ctrl Pts',(-16.6976654942767,-19.5308638594846,
5.72633916638811));
#162436=CARTESIAN_POINT('Ctrl Pts',(-16.6996603447386,-19.5378359476061,
5.72677288082037));
#162437=CARTESIAN_POINT('Ctrl Pts',(-16.7108434076673,-19.5761752274405,
5.72915069929992));
#162438=CARTESIAN_POINT('Ctrl Pts',(-16.7207218191578,-19.6073384954114,
5.73105701045006));
#162439=CARTESIAN_POINT('Ctrl Pts',(-16.784013906238,-19.7920402849525,
5.74226543886967));
#162440=CARTESIAN_POINT('Ctrl Pts',(-16.8542508862671,-19.9392530083768,
5.75085776160672));
#162441=CARTESIAN_POINT('Ctrl Pts',(-17.0027194984562,-20.1759273173352,
5.76615304170199));
#162442=CARTESIAN_POINT('Ctrl Pts',(-17.0728581933659,-20.2695480614537,
5.77267334289562));
#162443=CARTESIAN_POINT('Ctrl Pts',(-17.1598351761568,-20.3675911473464,
5.78035144233042));
#162444=CARTESIAN_POINT('Ctrl Pts',(-17.1694258859234,-20.3781840749792,
5.78119292552645));
#162445=CARTESIAN_POINT('Ctrl Pts',(-17.1848605383916,-20.3948885641239,
5.78253947318229));
#162446=CARTESIAN_POINT('Ctrl Pts',(-17.1906352321315,-20.4010637219014,
5.78304159666562));
#162447=CARTESIAN_POINT('Ctrl Pts',(-17.2008850422826,-20.4118935635214,
5.78393000078321));
#162448=CARTESIAN_POINT('Ctrl Pts',(-17.2053447793969,-20.416562701111,
5.78431561543046));
#162449=CARTESIAN_POINT('Ctrl Pts',(-17.2146131852289,-20.4261778361843,
5.78511513420377));
#162450=CARTESIAN_POINT('Ctrl Pts',(-17.2194248029293,-20.4311208727698,
5.78552916471337));
#162451=CARTESIAN_POINT('Ctrl Pts',(-17.2318378015758,-20.4437488286995,
5.78659469671665));
#162452=CARTESIAN_POINT('Ctrl Pts',(-17.2394739679688,-20.4513991366863,
5.78724772783286));
#162453=CARTESIAN_POINT('Ctrl Pts',(-17.2715919344855,-20.4830874657198,
5.78998451671004));
#162454=CARTESIAN_POINT('Ctrl Pts',(-17.2965965758149,-20.5065859119125,
5.79209162134595));
#162455=CARTESIAN_POINT('Ctrl Pts',(-17.3632291513305,-20.566222423206,
5.79764995273216));
#162456=CARTESIAN_POINT('Ctrl Pts',(-17.4057149383756,-20.6013588829749,
5.80113963136773));
#162457=CARTESIAN_POINT('Ctrl Pts',(-17.5364854946473,-20.7011761845427,
5.81171414833407));
#162458=CARTESIAN_POINT('Ctrl Pts',(-17.6284596213665,-20.7607109555451,
5.81894736091875));
#162459=CARTESIAN_POINT('Ctrl Pts',(-17.8286596664689,-20.8693050643782,
5.83399225978492));
#162460=CARTESIAN_POINT('Ctrl Pts',(-17.9372687529282,-20.9169238339103,
5.84177589648977));
#162461=CARTESIAN_POINT('Ctrl Pts',(-18.0583209110286,-20.9582994912081,
5.84967761096853));
#162462=CARTESIAN_POINT('Ctrl Pts',(-18.0673625331739,-20.9613218695196,
5.85026323333849));
#162463=CARTESIAN_POINT('Ctrl Pts',(-18.0807854438123,-20.9657082193506,
5.85112554954407));
#162464=CARTESIAN_POINT('Ctrl Pts',(-18.0851511010813,-20.9671191419822,
5.85140490399214));
#162465=CARTESIAN_POINT('Ctrl Pts',(-18.0929242660442,-20.9696034461522,
5.8519002953606));
#162466=CARTESIAN_POINT('Ctrl Pts',(-18.0963299317984,-20.9706824037902,
5.85211665638576));
#162467=CARTESIAN_POINT('Ctrl Pts',(-18.1036551236241,-20.9729827288844,
5.85258054341281));
#162468=CARTESIAN_POINT('Ctrl Pts',(-18.1075754644813,-20.974201314306,
5.85282790564607));
#162469=CARTESIAN_POINT('Ctrl Pts',(-18.1183999969435,-20.9775314764298,
5.85350847531314));
#162470=CARTESIAN_POINT('Ctrl Pts',(-18.1253115585935,-20.9796191729427,
5.85394030648065));
#162471=CARTESIAN_POINT('Ctrl Pts',(-18.1631243408226,-20.9908300782805,
5.85628868661778));
#162472=CARTESIAN_POINT('Ctrl Pts',(-18.1942218783975,-20.9992828189253,
5.85816853705458));
#162473=CARTESIAN_POINT('Ctrl Pts',(-18.383680714159,-21.0461627927648,
5.8693785749537));
#162474=CARTESIAN_POINT('Ctrl Pts',(-18.5458657190907,-21.0669134396363,
5.87799093693147));
#162475=CARTESIAN_POINT('Ctrl Pts',(-18.8257554460276,-21.0702400933843,
5.89331411136127));
#162476=CARTESIAN_POINT('Ctrl Pts',(-18.9425694519663,-21.0619416269869,
5.8998411419959));
#162477=CARTESIAN_POINT('Ctrl Pts',(-19.0722153176857,-21.0418573243487,
5.90752681667408));
#162478=CARTESIAN_POINT('Ctrl Pts',(-19.0863152331751,-21.0395265743963,
5.90836839777694));
#162479=CARTESIAN_POINT('Ctrl Pts',(-19.1087176984666,-21.0355899631908,
5.90971507283278));
#162480=CARTESIAN_POINT('Ctrl Pts',(-19.1170362441381,-21.0340767807088,
5.91021722492811));
#162481=CARTESIAN_POINT('Ctrl Pts',(-19.1316910170746,-21.0313202125601,
5.91110566237399));
#162482=CARTESIAN_POINT('Ctrl Pts',(-19.1380310740476,-21.0300975870255,
5.91149128157707));
#162483=CARTESIAN_POINT('Ctrl Pts',(-19.1511325799385,-21.0275088517307,
5.91229079281219));
#162484=CARTESIAN_POINT('Ctrl Pts',(-19.1578931359694,-21.0261386622848,
5.91270481114415));
#162485=CARTESIAN_POINT('Ctrl Pts',(-19.1752290944058,-21.0225368156599,
5.91377027603383));
#162486=CARTESIAN_POINT('Ctrl Pts',(-19.1857942253928,-21.0202571865874,
5.91442325184223));
#162487=CARTESIAN_POINT('Ctrl Pts',(-19.2298154035022,-21.0104053836241,
5.91715950466795));
#162488=CARTESIAN_POINT('Ctrl Pts',(-19.2631008442643,-21.002101879917,
5.91926611712376));
#162489=CARTESIAN_POINT('Ctrl Pts',(-19.3492886245532,-20.9783624408507,
5.92482284071704));
#162490=CARTESIAN_POINT('Ctrl Pts',(-19.4018134129606,-20.9616639664461,
5.92831137601296));
#162491=CARTESIAN_POINT('Ctrl Pts',(-19.6495371044364,-20.8721242887725,
5.94524250178755));
#162492=CARTESIAN_POINT('Ctrl Pts',(-19.8338993122075,-20.7727948994148,
5.95943299137011));
#162493=CARTESIAN_POINT('Ctrl Pts',(-20.0044076837944,-20.6454502673376,
5.97284947527249));
#162494=CARTESIAN_POINT('Ctrl Pts',(-20.0080258472485,-20.6427299110824,
5.97313425506109));
#162495=CARTESIAN_POINT('Ctrl Pts',(-20.0280037889704,-20.6276087295909,
5.97470702797371));
#162496=CARTESIAN_POINT('Ctrl Pts',(-20.0441919305309,-20.6149815386789,
5.97598272523516));
#162497=CARTESIAN_POINT('Ctrl Pts',(-20.0652189160412,-20.5980822423302,
5.9776386286751));
#162498=CARTESIAN_POINT('Ctrl Pts',(-20.0702249333119,-20.594021157299,
5.97803277399033));
#162499=CARTESIAN_POINT('Ctrl Pts',(-20.078255760117,-20.5874451759944,
5.9786648286444));
#162500=CARTESIAN_POINT('Ctrl Pts',(-20.0812922001731,-20.5849446408951,
5.97890374995387));
#162501=CARTESIAN_POINT('Ctrl Pts',(-20.0869640603339,-20.5802472240868,
5.97934990184067));
#162502=CARTESIAN_POINT('Ctrl Pts',(-20.0896011096847,-20.5780523985531,
5.97955727488255));
#162503=CARTESIAN_POINT('Ctrl Pts',(-20.0958374887617,-20.5728361231763,
5.98004757816586));
#162504=CARTESIAN_POINT('Ctrl Pts',(-20.0994321377805,-20.5698090623061,
5.98033009954665));
#162505=CARTESIAN_POINT('Ctrl Pts',(-20.1106650327052,-20.5602857117942,
5.98121277586101));
#162506=CARTESIAN_POINT('Ctrl Pts',(-20.1182673520699,-20.5537469993475,
5.98180991118469));
#162507=CARTESIAN_POINT('Ctrl Pts',(-20.1360931391857,-20.5381934312686,
5.9832102571503));
#162508=CARTESIAN_POINT('Ctrl Pts',(-20.1462766852041,-20.5291332717567,
5.98401040178967));
#162509=CARTESIAN_POINT('Ctrl Pts',(-20.1816923608735,-20.4970063112347,
5.9867965794332));
#162510=CARTESIAN_POINT('Ctrl Pts',(-20.2064537415239,-20.4734262727678,
5.98875090838179));
#162511=CARTESIAN_POINT('Ctrl Pts',(-20.2843263290296,-20.3955859953749,
5.99496002150858));
#162512=CARTESIAN_POINT('Ctrl Pts',(-20.3350957616044,-20.3390637948339,
5.99910803332371));
#162513=CARTESIAN_POINT('Ctrl Pts',(-20.4906342492996,-20.1459519721364,
6.01259284077695));
#162514=CARTESIAN_POINT('Ctrl Pts',(-20.5818013463658,-19.9993340180964,
6.02185806072684));
#162515=CARTESIAN_POINT('Ctrl Pts',(-20.6640048104395,-19.8222356646158,
6.03320084879666));
#162516=CARTESIAN_POINT('Ctrl Pts',(-20.6734378130662,-19.8010050569571,
6.03456163412833));
#162517=CARTESIAN_POINT('Ctrl Pts',(-20.6862667133323,-19.7708012979155,
6.03650078366958));
#162518=CARTESIAN_POINT('Ctrl Pts',(-20.6899541465969,-19.7619532438794,
6.03706923108221));
#162519=CARTESIAN_POINT('Ctrl Pts',(-20.6958419147377,-19.7475507467972,
6.03799526562721));
#162520=CARTESIAN_POINT('Ctrl Pts',(-20.6980790779002,-19.742011432689,
6.03835160206131));
#162521=CARTESIAN_POINT('Ctrl Pts',(-20.7027082021864,-19.7304083153777,
6.0390984161855));
#162522=CARTESIAN_POINT('Ctrl Pts',(-20.7050956594865,-19.7243427933783,
6.03948904107576));
#162523=CARTESIAN_POINT('Ctrl Pts',(-20.7107003759924,-19.7099083145188,
6.04041922051662));
#162524=CARTESIAN_POINT('Ctrl Pts',(-20.7138925368234,-19.701529804898,
6.04095961076518));
#162525=CARTESIAN_POINT('Ctrl Pts',(-20.724429857036,-19.6733352943484,
6.04277978457929));
#162526=CARTESIAN_POINT('Ctrl Pts',(-20.73153131129,-19.6534301335466,6.04406765108529));
#162527=CARTESIAN_POINT('Ctrl Pts',(-20.7683471023197,-19.5451403217933,
6.05109146810279));
#162528=CARTESIAN_POINT('Ctrl Pts',(-20.7924915414983,-19.4549832624818,
6.05700835583422));
#162529=CARTESIAN_POINT('Ctrl Pts',(-20.8375614576733,-19.2275614183288,
6.07205891368725));
#162530=CARTESIAN_POINT('Ctrl Pts',(-20.8510859073101,-19.0892811223752,
6.0813351986236));
#162531=CARTESIAN_POINT('Ctrl Pts',(-20.8509995894478,-18.9506815623441,
6.09037079128207));
#162532=CARTESIAN_POINT('Ctrl Pts',(-20.7225805737622,-18.2258896078036,
6.13370788795281));
#162533=CARTESIAN_POINT('Ctrl Pts',(-20.7475745958775,-18.2943401180468,
6.1293268890434));
#162534=CARTESIAN_POINT('Ctrl Pts',(-20.7690040532235,-18.3640107463775,
6.124945890134));
#162535=CARTESIAN_POINT('Ctrl Pts',(-20.7867732913512,-18.4344955900524,
6.1205648912246));
#162536=CARTESIAN_POINT('Ctrl Pts',(-20.8045716030756,-18.5050957593199,
6.11617672423098));
#162537=CARTESIAN_POINT('Ctrl Pts',(-20.8186976575299,-18.5765123291963,
6.11178855723736));
#162538=CARTESIAN_POINT('Ctrl Pts',(-20.8291072241906,-18.648331234493,
6.10740039024374));
#162539=CARTESIAN_POINT('Ctrl Pts',(-20.8314491053219,-18.6644886159353,
6.10641316706544));
#162540=CARTESIAN_POINT('Ctrl Pts',(-20.8336030915946,-18.6806663528588,
6.10542594388715));
#162541=CARTESIAN_POINT('Ctrl Pts',(-20.8355690425741,-18.6968597262404,
6.10443872070886));
#162542=CARTESIAN_POINT('Ctrl Pts',(-20.8457798800574,-18.7809655384569,
6.09931124014674));
#162543=CARTESIAN_POINT('Ctrl Pts',(-20.8509432233709,-18.8656963446802,
6.09418375958462));
#162544=CARTESIAN_POINT('Ctrl Pts',(-20.8509995343428,-18.9505958660381,
6.0890562790225));
#162545=CARTESIAN_POINT('Origin',(-18.734,-18.952,0.));
#162546=CARTESIAN_POINT('',(-20.7225806193429,-18.2258897326344,7.15616144973347));
#162547=CARTESIAN_POINT('',(-20.7193262654686,-18.2270707613317,6.9336185967496));
#162548=CARTESIAN_POINT('',(-20.7225805737622,-18.2258896078036,0.));
#162549=CARTESIAN_POINT('Ctrl Pts',(-20.722580619343,-18.2258897326345,
7.15616144973347));
#162550=CARTESIAN_POINT('Ctrl Pts',(-20.7474159485307,-18.2939056477337,
7.15141143636792));
#162551=CARTESIAN_POINT('Ctrl Pts',(-20.7687705305159,-18.3632196853033,
7.14660731423374));
#162552=CARTESIAN_POINT('Ctrl Pts',(-20.8048202395505,-18.5059446662293,
7.13689825333913));
#162553=CARTESIAN_POINT('Ctrl Pts',(-20.8192617789026,-18.579244489578,
7.13200648739265));
#162554=CARTESIAN_POINT('Ctrl Pts',(-20.8346727925628,-18.6873232489186,
7.12505663315095));
#162555=CARTESIAN_POINT('Ctrl Pts',(-20.8387085643111,-18.7216043817949,
7.12289068190063));
#162556=CARTESIAN_POINT('Ctrl Pts',(-20.8425871760633,-18.7633111958887,
7.1203142244639));
#162557=CARTESIAN_POINT('Ctrl Pts',(-20.8432314561933,-18.7706549925183,
7.11986276020787));
#162558=CARTESIAN_POINT('Ctrl Pts',(-20.8441775336876,-18.7821267974974,
7.11916111919254));
#162559=CARTESIAN_POINT('Ctrl Pts',(-20.8445056016048,-18.786252496608,
7.11890950763311));
#162560=CARTESIAN_POINT('Ctrl Pts',(-20.8450939761029,-18.7939368625231,
7.11844224978327));
#162561=CARTESIAN_POINT('Ctrl Pts',(-20.8453573821261,-18.7974951891836,
7.11822643729257));
#162562=CARTESIAN_POINT('Ctrl Pts',(-20.8459354331439,-18.8055816661404,
7.11773724110973));
#162563=CARTESIAN_POINT('Ctrl Pts',(-20.8462445116671,-18.8101101621952,
7.11746417234176));
#162564=CARTESIAN_POINT('Ctrl Pts',(-20.8470081047971,-18.8218538747789,
7.11675823947325));
#162565=CARTESIAN_POINT('Ctrl Pts',(-20.8474402333973,-18.8290705564333,
7.11632659938544));
#162566=CARTESIAN_POINT('Ctrl Pts',(-20.8499256633052,-18.874475134017,
7.11362371524834));
#162567=CARTESIAN_POINT('Ctrl Pts',(-20.8509809806051,-18.9127131807723,
7.11140447444166));
#162568=CARTESIAN_POINT('Ctrl Pts',(-20.85107929024,-19.1130991834192,7.09997632154619));
#162569=CARTESIAN_POINT('Ctrl Pts',(-20.832532272912,-19.2747232960159,
7.09141467905363));
#162570=CARTESIAN_POINT('Ctrl Pts',(-20.7706268575478,-19.5402576310947,
7.07645440730754));
#162571=CARTESIAN_POINT('Ctrl Pts',(-20.7371602834163,-19.6457147998709,
7.07026714313349));
#162572=CARTESIAN_POINT('Ctrl Pts',(-20.6902873299116,-19.7612157374525,
7.06296374493082));
#162573=CARTESIAN_POINT('Ctrl Pts',(-20.6848211896208,-19.7743058424031,
7.06212830387132));
#162574=CARTESIAN_POINT('Ctrl Pts',(-20.6758998531024,-19.7950806194622,
7.06078962050351));
#162575=CARTESIAN_POINT('Ctrl Pts',(-20.6725295620061,-19.802801448336,
7.06028926503449));
#162576=CARTESIAN_POINT('Ctrl Pts',(-20.6664968922424,-19.8163994380094,
7.05940291807479));
#162577=CARTESIAN_POINT('Ctrl Pts',(-20.6638535463615,-19.8222849620273,
7.05901758266764));
#162578=CARTESIAN_POINT('Ctrl Pts',(-20.6583232650024,-19.8344492783238,
7.05821758675019));
#162579=CARTESIAN_POINT('Ctrl Pts',(-20.6554324100129,-19.840726194637,
7.05780279464393));
#162580=CARTESIAN_POINT('Ctrl Pts',(-20.6479172891203,-19.856835716409,
7.05673306750295));
#162581=CARTESIAN_POINT('Ctrl Pts',(-20.6432480051394,-19.8666469872364,
7.05607657953998));
#162582=CARTESIAN_POINT('Ctrl Pts',(-20.6233051551381,-19.9077334582909,
7.05330608146364));
#162583=CARTESIAN_POINT('Ctrl Pts',(-20.6073377344372,-19.9386640357421,
7.05116799924515));
#162584=CARTESIAN_POINT('Ctrl Pts',(-20.5636050720558,-20.0184869853972,
7.04550815445178));
#162585=CARTESIAN_POINT('Ctrl Pts',(-20.5346433172842,-20.0666891878495,
7.04194616612573));
#162586=CARTESIAN_POINT('Ctrl Pts',(-20.4347648079773,-20.2188525683532,
7.03023634280935));
#162587=CARTESIAN_POINT('Ctrl Pts',(-20.3564958450735,-20.3176569597721,
7.02187690373839));
#162588=CARTESIAN_POINT('Ctrl Pts',(-20.2011025010974,-20.4814773474229,
7.00699941111169));
#162589=CARTESIAN_POINT('Ctrl Pts',(-20.1272128747746,-20.5490764986592,
7.00047982678317));
#162590=CARTESIAN_POINT('Ctrl Pts',(-20.0412146205106,-20.6172245824404,
6.99370044053259));
#162591=CARTESIAN_POINT('Ctrl Pts',(-20.0335754764066,-20.6231931556124,
6.99310480878766));
#162592=CARTESIAN_POINT('Ctrl Pts',(-20.0222359687522,-20.631928101703,
6.99223065053106));
#162593=CARTESIAN_POINT('Ctrl Pts',(-20.0185672425278,-20.6347350767237,
6.99194935860015));
#162594=CARTESIAN_POINT('Ctrl Pts',(-20.0120424365153,-20.6396934898453,
6.99145183254905));
#162595=CARTESIAN_POINT('Ctrl Pts',(-20.0091900671574,-20.6418497206862,
6.9912352635893));
#162596=CARTESIAN_POINT('Ctrl Pts',(-20.0030671641756,-20.6464539595855,
6.99077237128944));
#162597=CARTESIAN_POINT('Ctrl Pts',(-19.9997950130008,-20.6488997242191,
6.99052620416663));
#162598=CARTESIAN_POINT('Ctrl Pts',(-19.9907938696364,-20.6555870922754,
6.98985228578299));
#162599=CARTESIAN_POINT('Ctrl Pts',(-19.9850504412018,-20.6598093010002,
6.98942586664614));
#162600=CARTESIAN_POINT('Ctrl Pts',(-19.9542778896278,-20.6821928073414,
6.98715963469539));
#162601=CARTESIAN_POINT('Ctrl Pts',(-19.9288730094435,-20.6998340873346,
6.9853535566624));
#162602=CARTESIAN_POINT('Ctrl Pts',(-19.8508165922211,-20.7515391271985,
6.97996808211128));
#162603=CARTESIAN_POINT('Ctrl Pts',(-19.7970274466996,-20.7838280943938,
6.9764754350482));
#162604=CARTESIAN_POINT('Ctrl Pts',(-19.6236648957386,-20.8776833345748,
6.96564106410738));
#162605=CARTESIAN_POINT('Ctrl Pts',(-19.4996237104855,-20.9302772723831,
6.95847231608247));
#162606=CARTESIAN_POINT('Ctrl Pts',(-19.3325235273573,-20.9830399688898,
6.94874727225968));
#162607=CARTESIAN_POINT('Ctrl Pts',(-19.2932700247087,-20.9941974835814,
6.94646003972938));
#162608=CARTESIAN_POINT('Ctrl Pts',(-19.2066105209316,-21.0161438746866,
6.94137929796329));
#162609=CARTESIAN_POINT('Ctrl Pts',(-19.1591071754183,-21.0264478774865,
6.93857399067379));
#162610=CARTESIAN_POINT('Ctrl Pts',(-19.0988926671266,-21.0373539690993,
6.93497497217654));
#162611=CARTESIAN_POINT('Ctrl Pts',(-19.0864718578771,-21.0394892608184,
6.93423032762956));
#162612=CARTESIAN_POINT('Ctrl Pts',(-19.0667599300631,-21.0426970431307,
6.9330447211818));
#162613=CARTESIAN_POINT('Ctrl Pts',(-19.0594808803921,-21.0438426067955,
6.93260608202739));
#162614=CARTESIAN_POINT('Ctrl Pts',(-19.0459068967655,-21.0459062910415,
6.93178650567151));
#162615=CARTESIAN_POINT('Ctrl Pts',(-19.0396135015102,-21.046834087521,
6.93140588011488));
#162616=CARTESIAN_POINT('Ctrl Pts',(-19.0256263817557,-21.048831750755,
6.93055847586553));
#162617=CARTESIAN_POINT('Ctrl Pts',(-19.0179307857528,-21.0498876623651,
6.93009126087912));
#162618=CARTESIAN_POINT('Ctrl Pts',(-18.9955533574643,-21.0528326837023,
6.92872975066363));
#162619=CARTESIAN_POINT('Ctrl Pts',(-18.9808575305314,-21.0546101554663,
6.92783194711667));
#162620=CARTESIAN_POINT('Ctrl Pts',(-18.8639365396358,-21.0675091868573,
6.92065857951775));
#162621=CARTESIAN_POINT('Ctrl Pts',(-18.7610580881093,-21.0713218368246,
6.91415219518838));
#162622=CARTESIAN_POINT('Ctrl Pts',(-18.5026308447506,-21.0620777466229,
6.89736605972563));
#162623=CARTESIAN_POINT('Ctrl Pts',(-18.3480413664539,-21.0393408915334,
6.88689581572453));
#162624=CARTESIAN_POINT('Ctrl Pts',(-18.1465345399949,-20.9865350700021,
6.8734399181643));
#162625=CARTESIAN_POINT('Ctrl Pts',(-18.0962268340151,-20.9713303349522,
6.87010209097466));
#162626=CARTESIAN_POINT('Ctrl Pts',(-18.0383148645933,-20.951446595531,
6.86632516179938));
#162627=CARTESIAN_POINT('Ctrl Pts',(-18.0301142028517,-20.948574387927,
6.86579189077599));
#162628=CARTESIAN_POINT('Ctrl Pts',(-18.0177156751048,-20.9441460299063,
6.86498826630709));
#162629=CARTESIAN_POINT('Ctrl Pts',(-18.0135047940447,-20.942626960937,
6.8647157940955));
#162630=CARTESIAN_POINT('Ctrl Pts',(-18.0059505413455,-20.9398746650922,
6.8642278528222));
#162631=CARTESIAN_POINT('Ctrl Pts',(-18.0026054525391,-20.9386463487209,
6.86401209794063));
#162632=CARTESIAN_POINT('Ctrl Pts',(-17.9953385797544,-20.9359571114531,
6.86354406999329));
#162633=CARTESIAN_POINT('Ctrl Pts',(-17.9914180340214,-20.9344930109192,
6.86329198980055));
#162634=CARTESIAN_POINT('Ctrl Pts',(-17.9804047731397,-20.9303429314,6.86258499645883));
#162635=CARTESIAN_POINT('Ctrl Pts',(-17.9733220304437,-20.9276304185608,
6.86213164126668));
#162636=CARTESIAN_POINT('Ctrl Pts',(-17.9308016347848,-20.9110836085839,
6.85941705979401));
#162637=CARTESIAN_POINT('Ctrl Pts',(-17.8957251652699,-20.89633328074,6.85720736574715));
#162638=CARTESIAN_POINT('Ctrl Pts',(-17.7810025906549,-20.8444079089298,
6.85001930078642));
#162639=CARTESIAN_POINT('Ctrl Pts',(-17.7032696104921,-20.8032182657645,
6.84521027761111));
#162640=CARTESIAN_POINT('Ctrl Pts',(-17.4797370737944,-20.6663133912096,
6.83095059804825));
#162641=CARTESIAN_POINT('Ctrl Pts',(-17.342976576592,-20.5573326669932,
6.82157759891172));
#162642=CARTESIAN_POINT('Ctrl Pts',(-17.2049681163796,-20.416337177459,
6.81011402251051));
#162643=CARTESIAN_POINT('Ctrl Pts',(-17.1890923458789,-20.3995780286448,
6.80876171758984));
#162644=CARTESIAN_POINT('Ctrl Pts',(-17.1670331032444,-20.3755150738235,
6.80683260898806));
#162645=CARTESIAN_POINT('Ctrl Pts',(-17.1606198708755,-20.3684234485663,
6.80626558163055));
#162646=CARTESIAN_POINT('Ctrl Pts',(-17.1502809925065,-20.3568340619956,
6.80534123164458));
#162647=CARTESIAN_POINT('Ctrl Pts',(-17.1463258988312,-20.3523626615249,
6.80498515058715));
#162648=CARTESIAN_POINT('Ctrl Pts',(-17.1380892593073,-20.3429710448187,
6.80423836051389));
#162649=CARTESIAN_POINT('Ctrl Pts',(-17.133811439374,-20.3380476574585,
6.8038475020388));
#162650=CARTESIAN_POINT('Ctrl Pts',(-17.123693571454,-20.3262936256549,
6.80291582507786));
#162651=CARTESIAN_POINT('Ctrl Pts',(-17.1178741681609,-20.319445448675,
6.80237416370403));
#162652=CARTESIAN_POINT('Ctrl Pts',(-17.0984378001158,-20.2962756799691,
6.80054525595321));
#162653=CARTESIAN_POINT('Ctrl Pts',(-17.0850234339455,-20.2797865213732,
6.79924982052421));
#162654=CARTESIAN_POINT('Ctrl Pts',(-17.0134816434154,-20.189089704933,
6.7921551194847));
#162655=CARTESIAN_POINT('Ctrl Pts',(-16.9601191198161,-20.1112742846567,
6.78617080228864));
#162656=CARTESIAN_POINT('Ctrl Pts',(-16.8276090706388,-19.8873609752444,
6.76927188331487));
#162657=CARTESIAN_POINT('Ctrl Pts',(-16.7601844296791,-19.7351188456599,
6.75808913236996));
#162658=CARTESIAN_POINT('Ctrl Pts',(-16.698839032824,-19.536442191861,6.74476022370512));
#162659=CARTESIAN_POINT('Ctrl Pts',(-16.6876443902823,-19.4959504574135,
6.74210928349517));
#162660=CARTESIAN_POINT('Ctrl Pts',(-16.6758934706876,-19.4479252253436,
6.73906266115482));
#162661=CARTESIAN_POINT('Ctrl Pts',(-16.6741638656779,-19.4406915372785,
6.73860635273242));
#162662=CARTESIAN_POINT('Ctrl Pts',(-16.6714258300277,-19.4289674733244,
6.73787112906865));
#162663=CARTESIAN_POINT('Ctrl Pts',(-16.6703938737201,-19.4244827338115,
6.73759091379964));
#162664=CARTESIAN_POINT('Ctrl Pts',(-16.6685864847603,-19.416509185568,
6.73709457584128));
#162665=CARTESIAN_POINT('Ctrl Pts',(-16.6678052557828,-19.4130217479148,
6.73687812427595));
#162666=CARTESIAN_POINT('Ctrl Pts',(-16.666147553022,-19.4055328397193,
6.73641468769454));
#162667=CARTESIAN_POINT('Ctrl Pts',(-16.665273862861,-19.4015308102332,
6.73616786306043));
#162668=CARTESIAN_POINT('Ctrl Pts',(-16.6629010393419,-19.3905084118941,
6.73549028719701));
#162669=CARTESIAN_POINT('Ctrl Pts',(-16.6614259736264,-19.3834828394061,
6.73506089228671));
#162670=CARTESIAN_POINT('Ctrl Pts',(-16.6536451994359,-19.3454631958638,
6.73274993296016));
#162671=CARTESIAN_POINT('Ctrl Pts',(-16.6479985872231,-19.3143364880446,
6.73090370057324));
#162672=CARTESIAN_POINT('Ctrl Pts',(-16.6174872737227,-19.1216487199776,
6.71969112518278));
#162673=CARTESIAN_POINT('Ctrl Pts',(-16.6107040475629,-18.9577698631849,
6.71105294674226));
#162674=CARTESIAN_POINT('Ctrl Pts',(-16.6315477823811,-18.6779717712427,
6.69569422906591));
#162675=CARTESIAN_POINT('Ctrl Pts',(-16.6499148071755,-18.5621533353466,
6.689158963228));
#162676=CARTESIAN_POINT('Ctrl Pts',(-16.6811576415342,-18.4345721822288,
6.68146401857769));
#162677=CARTESIAN_POINT('Ctrl Pts',(-16.6846978352459,-18.4207242543374,
6.6806223194999));
#162678=CARTESIAN_POINT('Ctrl Pts',(-16.6905550899693,-18.3987429188184,
6.6792754909367));
#162679=CARTESIAN_POINT('Ctrl Pts',(-16.6927811668969,-18.3905855626823,
6.67877330437085));
#162680=CARTESIAN_POINT('Ctrl Pts',(-16.6967932184971,-18.3762229406559,
6.67788482677648));
#162681=CARTESIAN_POINT('Ctrl Pts',(-16.6985588353912,-18.370012064851,
6.67749920208878));
#162682=CARTESIAN_POINT('Ctrl Pts',(-16.7022693175634,-18.357183210052,
6.67669969994454));
#162683=CARTESIAN_POINT('Ctrl Pts',(-16.7042181670829,-18.3505664720304,
6.67628569628896));
#162684=CARTESIAN_POINT('Ctrl Pts',(-16.7093033190877,-18.333607612024,
6.67522031226337));
#162685=CARTESIAN_POINT('Ctrl Pts',(-16.7124865134754,-18.3232798617662,
6.67456740309062));
#162686=CARTESIAN_POINT('Ctrl Pts',(-16.7260999477913,-18.2802840126132,
6.67183179590795));
#162687=CARTESIAN_POINT('Ctrl Pts',(-16.7372436301281,-18.2478489006737,
6.66972577622967));
#162688=CARTESIAN_POINT('Ctrl Pts',(-16.7683257651038,-18.1640613433321,
6.6641709888208));
#162689=CARTESIAN_POINT('Ctrl Pts',(-16.7894883502945,-18.1131936166144,
6.66068383030605));
#162690=CARTESIAN_POINT('Ctrl Pts',(-16.8585268527179,-17.963945438486,
6.65011415425016));
#162691=CARTESIAN_POINT('Ctrl Pts',(-16.9120657266473,-17.8683933463588,
6.64288324632428));
#162692=CARTESIAN_POINT('Ctrl Pts',(-16.9983229424886,-17.7390531414224,
6.63261364002144));
#162693=CARTESIAN_POINT('Ctrl Pts',(-17.0251521824694,-17.7015383797828,
6.62957356358089));
#162694=CARTESIAN_POINT('Ctrl Pts',(-17.0664521983726,-17.6476037828493,
6.62513720610868));
#162695=CARTESIAN_POINT('Ctrl Pts',(-17.0799861851478,-17.6304843897788,
6.62371888947913));
#162696=CARTESIAN_POINT('Ctrl Pts',(-17.126476016809,-17.5735118039761,
6.61897158594626));
#162697=CARTESIAN_POINT('Ctrl Pts',(-17.1606293566649,-17.5346542989865,
6.61568756123581));
#162698=CARTESIAN_POINT('Ctrl Pts',(-17.2021187341105,-17.4908006308627,
6.61196399656109));
#162699=CARTESIAN_POINT('Ctrl Pts',(-17.2081015151472,-17.4845540456529,
6.61143318642979));
#162700=CARTESIAN_POINT('Ctrl Pts',(-17.2172326532883,-17.475136506644,
6.61063252802957));
#162701=CARTESIAN_POINT('Ctrl Pts',(-17.2203529583771,-17.4719386511729,
6.61036058386553));
#162702=CARTESIAN_POINT('Ctrl Pts',(-17.2259797304643,-17.4662084394985,
6.60987320464635));
#162703=CARTESIAN_POINT('Ctrl Pts',(-17.2284824748074,-17.4636725237711,
6.60965748672217));
#162704=CARTESIAN_POINT('Ctrl Pts',(-17.2339435489004,-17.4581669392718,
6.60918909743202));
#162705=CARTESIAN_POINT('Ctrl Pts',(-17.2369042902398,-17.4551997440116,
6.6089366213376));
#162706=CARTESIAN_POINT('Ctrl Pts',(-17.2452686041947,-17.4468668432311,
6.60822739699985));
#162707=CARTESIAN_POINT('Ctrl Pts',(-17.2506924063789,-17.4415214085732,
6.60777222252185));
#162708=CARTESIAN_POINT('Ctrl Pts',(-17.2837761102591,-17.4092657771348,
6.60502337312307));
#162709=CARTESIAN_POINT('Ctrl Pts',(-17.312140628635,-17.3830849088749,
6.6027827550018));
#162710=CARTESIAN_POINT('Ctrl Pts',(-17.4090490661397,-17.2984253421442,
6.59544164085161));
#162711=CARTESIAN_POINT('Ctrl Pts',(-17.4806105560092,-17.2435440871131,
6.59051881974452));
#162712=CARTESIAN_POINT('Ctrl Pts',(-17.6976217286544,-17.0981129854688,
6.5763138038528));
#162713=CARTESIAN_POINT('Ctrl Pts',(-17.8507966505464,-17.0204405360757,
6.56709270672974));
#162714=CARTESIAN_POINT('Ctrl Pts',(-18.0335325100814,-16.9541069793512,
6.55579954157498));
#162715=CARTESIAN_POINT('Ctrl Pts',(-18.0555496922783,-16.9465234124758,
6.55443559976432));
#162716=CARTESIAN_POINT('Ctrl Pts',(-18.0868088812237,-16.9363302068524,
6.55249271091416));
#162717=CARTESIAN_POINT('Ctrl Pts',(-18.0959508973042,-16.9334177259339,
6.55192373319032));
#162718=CARTESIAN_POINT('Ctrl Pts',(-18.1108182146862,-16.9287923558517,
6.55099706933841));
#162719=CARTESIAN_POINT('Ctrl Pts',(-18.1165315909493,-16.9270413654635,
6.55064063732268));
#162720=CARTESIAN_POINT('Ctrl Pts',(-18.128491341023,-16.9234313576681,
6.54989381294908));
#162721=CARTESIAN_POINT('Ctrl Pts',(-18.1347390306244,-16.9215769500281,
6.54950327423074));
#162722=CARTESIAN_POINT('Ctrl Pts',(-18.1495948171405,-16.9172420699767,
6.54857364889595));
#162723=CARTESIAN_POINT('Ctrl Pts',(-18.1582102405747,-16.9147873452604,
6.54803372924014));
#162724=CARTESIAN_POINT('Ctrl Pts',(-18.1871582354442,-16.9067377189396,
6.54621678123807));
#162725=CARTESIAN_POINT('Ctrl Pts',(-18.2075582674424,-16.9013920985435,
6.54493170895828));
#162726=CARTESIAN_POINT('Ctrl Pts',(-18.318213348977,-16.8741560662726,
6.53793396240243));
#162727=CARTESIAN_POINT('Ctrl Pts',(-18.4097434897625,-16.8579207924823,
6.53204185130024));
#162728=CARTESIAN_POINT('Ctrl Pts',(-18.6541350599363,-16.8309798409634,
6.51608371700417));
#162729=CARTESIAN_POINT('Ctrl Pts',(-18.8075946250902,-16.8307538985654,
6.50580706520825));
#162730=CARTESIAN_POINT('Ctrl Pts',(-18.9632351482536,-16.8474447845651,
6.49567693293862));
#162731=CARTESIAN_POINT('Ctrl Pts',(-18.9667366381847,-16.8478291263617,
6.4954492078278));
#162732=CARTESIAN_POINT('Ctrl Pts',(-19.0220450172929,-16.8540398083499,
6.49185506141242));
#162733=CARTESIAN_POINT('Ctrl Pts',(-19.0736251474451,-16.8617697178967,
6.48854338203455));
#162734=CARTESIAN_POINT('Ctrl Pts',(-19.133389701869,-16.8729973576294,
6.48479253461922));
#162735=CARTESIAN_POINT('Ctrl Pts',(-19.1418981825888,-16.8746499574007,
6.48426060598984));
#162736=CARTESIAN_POINT('Ctrl Pts',(-19.1547808663651,-16.8772343603836,
6.48345859933204));
#162737=CARTESIAN_POINT('Ctrl Pts',(-19.1591625423258,-16.8781278220961,
6.4831864150276));
#162738=CARTESIAN_POINT('Ctrl Pts',(-19.1670304680933,-16.8797581439452,
6.48269878038706));
#162739=CARTESIAN_POINT('Ctrl Pts',(-19.1705177009885,-16.8804899243351,
6.48248304583965));
#162740=CARTESIAN_POINT('Ctrl Pts',(-19.1781002693348,-16.8821010906249,
6.4820148217156));
#162741=CARTESIAN_POINT('Ctrl Pts',(-19.1821948343801,-16.8829838242807,
6.48176252631655));
#162742=CARTESIAN_POINT('Ctrl Pts',(-19.193712245762,-16.8855026190406,
6.48105432052355));
#162743=CARTESIAN_POINT('Ctrl Pts',(-19.2011290262645,-16.8871665318466,
6.48059997666856));
#162744=CARTESIAN_POINT('Ctrl Pts',(-19.2459000188025,-16.8974642290223,
6.47786684434423));
#162745=CARTESIAN_POINT('Ctrl Pts',(-19.2830255556427,-16.9070720752472,
6.47564041051448));
#162746=CARTESIAN_POINT('Ctrl Pts',(-19.4054604833123,-16.9423326758004,
6.4683698059703));
#162747=CARTESIAN_POINT('Ctrl Pts',(-19.4894150684498,-16.9723605058998,
6.46349944852714));
#162748=CARTESIAN_POINT('Ctrl Pts',(-19.7296489574193,-17.0758016402394,
6.44927415173421));
#162749=CARTESIAN_POINT('Ctrl Pts',(-19.8791157218193,-17.1631064012878,
6.43998766499431));
#162750=CARTESIAN_POINT('Ctrl Pts',(-20.034837646509,-17.2816553579202,
6.42861811600396));
#162751=CARTESIAN_POINT('Ctrl Pts',(-20.053107179289,-17.2960452927523,
6.42725593427173));
#162752=CARTESIAN_POINT('Ctrl Pts',(-20.0785701367534,-17.3167898882346,
6.42531513063309));
#162753=CARTESIAN_POINT('Ctrl Pts',(-20.0859634964498,-17.3228972831839,
6.42474644874198));
#162754=CARTESIAN_POINT('Ctrl Pts',(-20.0978954230114,-17.3328909941076,
6.42382013596474));
#162755=CARTESIAN_POINT('Ctrl Pts',(-20.1024595334296,-17.3367467065156,
6.42346375728607));
#162756=CARTESIAN_POINT('Ctrl Pts',(-20.1116179597681,-17.3445503273064,
6.42274446087752));
#162757=CARTESIAN_POINT('Ctrl Pts',(-20.1162117738043,-17.3484987357373,
6.42238152439874));
#162758=CARTESIAN_POINT('Ctrl Pts',(-20.1272067033567,-17.3580312931585,
6.42150766455482));
#162759=CARTESIAN_POINT('Ctrl Pts',(-20.1335912406369,-17.363634326575,
6.42099595856163));
#162760=CARTESIAN_POINT('Ctrl Pts',(-20.1538565176832,-17.3816360707754,
6.41935791814395));
#162761=CARTESIAN_POINT('Ctrl Pts',(-20.1676072518525,-17.3941792100084,
6.41822552815957));
#162762=CARTESIAN_POINT('Ctrl Pts',(-20.1994325006941,-17.423987797385,
6.41555440128884));
#162763=CARTESIAN_POINT('Ctrl Pts',(-20.2173698622435,-17.4413949973026,
6.41400970227844));
#162764=CARTESIAN_POINT('Ctrl Pts',(-20.2794071962141,-17.5037693195756,
6.40852584072723));
#162765=CARTESIAN_POINT('Ctrl Pts',(-20.3218016500598,-17.5503794252057,
6.40451740357261));
#162766=CARTESIAN_POINT('Ctrl Pts',(-20.4216783127836,-17.6705429157315,
6.39441378287514));
#162767=CARTESIAN_POINT('Ctrl Pts',(-20.4764941116557,-17.74613819415,6.38825018154735));
#162768=CARTESIAN_POINT('Ctrl Pts',(-20.5913660343305,-17.9288219018111,
6.37399161457688));
#162769=CARTESIAN_POINT('Ctrl Pts',(-20.6474684169153,-18.0380265199528,
6.3659192469899));
#162770=CARTESIAN_POINT('Ctrl Pts',(-20.6973852263465,-18.1602318655953,
6.35776677957427));
#162771=CARTESIAN_POINT('Ctrl Pts',(-20.7009005364253,-18.1690053556247,
6.35718624725605));
#162772=CARTESIAN_POINT('Ctrl Pts',(-20.7060289959388,-18.1820574430397,
6.35632996090637));
#162773=CARTESIAN_POINT('Ctrl Pts',(-20.7076871756968,-18.1863180586969,
6.35605159884923));
#162774=CARTESIAN_POINT('Ctrl Pts',(-20.7106159147882,-18.1939160487537,
6.3555572949701));
#162775=CARTESIAN_POINT('Ctrl Pts',(-20.7118918421534,-18.1972512914062,
6.3553410345474));
#162776=CARTESIAN_POINT('Ctrl Pts',(-20.7146202937716,-18.2044378330701,
6.35487661086278));
#162777=CARTESIAN_POINT('Ctrl Pts',(-20.7160700229184,-18.2082901328902,
6.35462861533865));
#162778=CARTESIAN_POINT('Ctrl Pts',(-20.719215033876,-18.2167217446924,
6.35408785900432));
#162779=CARTESIAN_POINT('Ctrl Pts',(-20.7209057282952,-18.2213027499434,
6.35379536866914));
#162780=CARTESIAN_POINT('Ctrl Pts',(-20.7225805737622,-18.2258896078036,
6.35350377396603));
#162781=CARTESIAN_POINT('',(-20.8509992748742,-18.9537521935255,6.8890562790225));
#162782=CARTESIAN_POINT('Ctrl Pts',(-20.8509992748742,-18.9537521935255,
6.8890562790225));
#162783=CARTESIAN_POINT('Ctrl Pts',(-20.8509006165464,-19.0729511321296,
6.88186870628082));
#162784=CARTESIAN_POINT('Ctrl Pts',(-20.8407310772906,-19.1917453566805,
6.87468113353914));
#162785=CARTESIAN_POINT('Ctrl Pts',(-20.8207141748805,-19.3088094062,6.86749356079746));
#162786=CARTESIAN_POINT('Ctrl Pts',(-20.8084933107471,-19.3802801969732,
6.86310535186656));
#162787=CARTESIAN_POINT('Ctrl Pts',(-20.7925724893355,-19.4512619171912,
6.85871714293567));
#162788=CARTESIAN_POINT('Ctrl Pts',(-20.7730042905686,-19.5213421669286,
6.85432893400477));
#162789=CARTESIAN_POINT('Ctrl Pts',(-20.7534651342531,-19.5913184059558,
6.8499472379035));
#162790=CARTESIAN_POINT('Ctrl Pts',(-20.7302894754046,-19.6603953697141,
6.84556554180223));
#162791=CARTESIAN_POINT('Ctrl Pts',(-20.7035811449958,-19.7281695132359,
6.84118384570097));
#162792=CARTESIAN_POINT('Ctrl Pts',(-20.6769041990008,-19.7958640167455,
6.83680729844133));
#162793=CARTESIAN_POINT('Ctrl Pts',(-20.6467030037517,-19.8622582946366,
6.83243075118168));
#162794=CARTESIAN_POINT('Ctrl Pts',(-20.6131310722287,-19.9269643139032,
6.82805420392204));
#162795=CARTESIAN_POINT('Ctrl Pts',(-20.5795804315367,-19.9916292975527,
6.82368043220507));
#162796=CARTESIAN_POINT('Ctrl Pts',(-20.5426635175973,-20.0546077198003,
6.81930666048809));
#162797=CARTESIAN_POINT('Ctrl Pts',(-20.5025812162808,-20.1155331887912,
6.81493288877111));
#162798=CARTESIAN_POINT('Ctrl Pts',(-20.4625111121433,-20.1764401179573,
6.81056044800756));
#162799=CARTESIAN_POINT('Ctrl Pts',(-20.4192777979153,-20.2352949313846,
6.806188007244));
#162800=CARTESIAN_POINT('Ctrl Pts',(-20.3731263263947,-20.2917588910397,
6.80181556648045));
#162801=CARTESIAN_POINT('Ctrl Pts',(-20.3269736747759,-20.3482242944844,
6.7974430139131));
#162802=CARTESIAN_POINT('Ctrl Pts',(-20.2779030245428,-20.4022983505562,
6.79307046134575));
#162803=CARTESIAN_POINT('Ctrl Pts',(-20.2261996115101,-20.4536755040318,
6.78869790877841));
#162804=CARTESIAN_POINT('Ctrl Pts',(-20.1744425387252,-20.5051059786551,
6.78432081821108));
#162805=CARTESIAN_POINT('Ctrl Pts',(-20.1200475906613,-20.5538336216567,
6.77994372764375));
#162806=CARTESIAN_POINT('Ctrl Pts',(-20.063336165121,-20.5995904709914,
6.77556663707642));
#162807=CARTESIAN_POINT('Ctrl Pts',(-20.0065937673663,-20.6453723098397,
6.77118715601747));
#162808=CARTESIAN_POINT('Ctrl Pts',(-19.9475327641504,-20.6881798414322,
6.76680767495853));
#162809=CARTESIAN_POINT('Ctrl Pts',(-19.8865046696906,-20.7277877086919,
6.76242819389958));
#162810=CARTESIAN_POINT('Ctrl Pts',(-19.8253684033431,-20.7674657806304,
6.75804095023986));
#162811=CARTESIAN_POINT('Ctrl Pts',(-19.7622585010735,-20.8039326211616,
6.75365370658014));
#162812=CARTESIAN_POINT('Ctrl Pts',(-19.6975517419863,-20.8370084987912,
6.74926646292041));
#162813=CARTESIAN_POINT('Ctrl Pts',(-19.6535573809358,-20.8594969083952,
6.74628355998562));
#162814=CARTESIAN_POINT('Ctrl Pts',(-19.6088253272205,-20.8804187619502,
6.74330065705082));
#162815=CARTESIAN_POINT('Ctrl Pts',(-19.5634785608968,-20.8997305555473,
6.74031775411602));
#162816=CARTESIAN_POINT('Ctrl Pts',(-19.4967680143858,-20.9281405262996,
6.73592954518512));
#162817=CARTESIAN_POINT('Ctrl Pts',(-19.4284659821153,-20.9531746938963,
6.73154133625421));
#162818=CARTESIAN_POINT('Ctrl Pts',(-19.3589476876738,-20.9746540454737,
6.72715312732331));
#162819=CARTESIAN_POINT('Ctrl Pts',(-19.2895325699076,-20.996101518132,
6.72277143122204));
#162820=CARTESIAN_POINT('Ctrl Pts',(-19.2189052304798,-21.014004507002,
6.71838973512076));
#162821=CARTESIAN_POINT('Ctrl Pts',(-19.1474611885819,-21.0282318862633,
6.71400803901949));
#162822=CARTESIAN_POINT('Ctrl Pts',(-19.0761010991189,-21.0424425472217,
6.70963149175985));
#162823=CARTESIAN_POINT('Ctrl Pts',(-19.0039266843573,-21.0529860848153,
6.70525494450021));
#162824=CARTESIAN_POINT('Ctrl Pts',(-18.9313473123123,-21.05978154426,6.70087839724056));
#162825=CARTESIAN_POINT('Ctrl Pts',(-18.8588139690502,-21.0665726941231,
6.69650462552358));
#162826=CARTESIAN_POINT('Ctrl Pts',(-18.7858766571606,-21.0696204372107,
6.6921308538066));
#162827=CARTESIAN_POINT('Ctrl Pts',(-18.7129521899221,-21.0688953657871,
6.68775708208963));
#162828=CARTESIAN_POINT('Ctrl Pts',(-18.6400499138438,-21.0681705150052,
6.68338464132607));
#162829=CARTESIAN_POINT('Ctrl Pts',(-18.5671609567207,-21.0636751337981,
6.67901220056251));
#162830=CARTESIAN_POINT('Ctrl Pts',(-18.4947027860638,-21.0554319203156,
6.67463975979895));
#162831=CARTESIAN_POINT('Ctrl Pts',(-18.4222427626436,-21.0471884960532,
6.67026720723161));
#162832=CARTESIAN_POINT('Ctrl Pts',(-18.3502140266194,-21.0351971057619,
6.66589465466426));
#162833=CARTESIAN_POINT('Ctrl Pts',(-18.2790278943154,-21.0195321963754,
6.66152210209691));
#162834=CARTESIAN_POINT('Ctrl Pts',(-18.2077678823583,-21.0038510293551,
6.65714501152958));
#162835=CARTESIAN_POINT('Ctrl Pts',(-18.1373526922054,-20.9844888351844,
6.65276792096224));
#162836=CARTESIAN_POINT('Ctrl Pts',(-18.0681816040656,-20.9615708157802,
6.64839083039491));
#162837=CARTESIAN_POINT('Ctrl Pts',(-17.9989727390273,-20.9386402799949,
6.64401134933596));
#162838=CARTESIAN_POINT('Ctrl Pts',(-17.9310097785365,-20.9121502278387,
6.63963186827702));
#162839=CARTESIAN_POINT('Ctrl Pts',(-17.8646724802103,-20.8822742456284,
6.63525238721807));
#162840=CARTESIAN_POINT('Ctrl Pts',(-17.798217599468,-20.8523453084401,
6.63086514355835));
#162841=CARTESIAN_POINT('Ctrl Pts',(-17.7333945644594,-20.8190186771211,
6.62647789989862));
#162842=CARTESIAN_POINT('Ctrl Pts',(-17.6705584443108,-20.7825138780226,
6.62209065623889));
#162843=CARTESIAN_POINT('Ctrl Pts',(-17.6278359374846,-20.7576941322301,
6.61910775330412));
#162844=CARTESIAN_POINT('Ctrl Pts',(-17.5860313573348,-20.7314061565717,
6.61612485036935));
#162845=CARTESIAN_POINT('Ctrl Pts',(-17.5452478505361,-20.7037298099721,
6.61314194743458));
#162846=CARTESIAN_POINT('Ctrl Pts',(-17.485250407548,-20.6630145758599,
6.60875373850369));
#162847=CARTESIAN_POINT('Ctrl Pts',(-17.4272300397248,-20.6191338958609,
6.60436552957279));
#162848=CARTESIAN_POINT('Ctrl Pts',(-17.3715403699669,-20.5723063773651,
6.5999773206419));
#162849=CARTESIAN_POINT('Ctrl Pts',(-17.3159333529124,-20.5255483586709,
6.59559562454064));
#162850=CARTESIAN_POINT('Ctrl Pts',(-17.2626505332034,-20.4758524915492,
6.59121392843937));
#162851=CARTESIAN_POINT('Ctrl Pts',(-17.2120162539404,-20.4234803691285,
6.58683223233811));
#162852=CARTESIAN_POINT('Ctrl Pts',(-17.1614414739852,-20.3711697881195,
6.58245568507847));
#162853=CARTESIAN_POINT('Ctrl Pts',(-17.1135093856056,-20.3161895440793,
6.57807913781884));
#162854=CARTESIAN_POINT('Ctrl Pts',(-17.0685096421061,-20.2588400314356,
6.5737025905592));
#162855=CARTESIAN_POINT('Ctrl Pts',(-17.0235384367899,-20.2015268890193,
6.56932881884223));
#162856=CARTESIAN_POINT('Ctrl Pts',(-16.9814961836088,-20.1418478378284,
6.56495504712526));
#162857=CARTESIAN_POINT('Ctrl Pts',(-16.9426332229367,-20.0801374340185,
6.56058127540829));
#162858=CARTESIAN_POINT('Ctrl Pts',(-16.9037820883941,-20.0184458088918,
6.55620883464474));
#162859=CARTESIAN_POINT('Ctrl Pts',(-16.8681085825374,-19.9547244662931,
6.55183639388119));
#162860=CARTESIAN_POINT('Ctrl Pts',(-16.8358195870607,-19.8893367164118,
6.54746395311764));
#162861=CARTESIAN_POINT('Ctrl Pts',(-16.8035297659509,-19.8239472945585,
6.5430914005503));
#162862=CARTESIAN_POINT('Ctrl Pts',(-16.7746248388303,-19.7568918142269,
6.53871884798296));
#162863=CARTESIAN_POINT('Ctrl Pts',(-16.7492648453343,-19.6885564240667,
6.53434629541562));
#162864=CARTESIAN_POINT('Ctrl Pts',(-16.7238785322805,-19.6201501128611,
6.5299692048483));
#162865=CARTESIAN_POINT('Ctrl Pts',(-16.7020446665442,-19.5504616929165,
6.52559211428097));
#162866=CARTESIAN_POINT('Ctrl Pts',(-16.6838740959313,-19.4798946651242,
6.52121502371365));
#162867=CARTESIAN_POINT('Ctrl Pts',(-16.6656936016954,-19.4092890980589,
6.51683554265471));
#162868=CARTESIAN_POINT('Ctrl Pts',(-16.6511804819229,-19.3378044408494,
6.51245606159577));
#162869=CARTESIAN_POINT('Ctrl Pts',(-16.6403943335874,-19.2658539685346,
6.50807658053683));
#162870=CARTESIAN_POINT('Ctrl Pts',(-16.6295890668764,-19.1937759644906,
6.50368933687712));
#162871=CARTESIAN_POINT('Ctrl Pts',(-16.6225240103777,-19.1212309770727,
6.4993020932174));
#162872=CARTESIAN_POINT('Ctrl Pts',(-16.6192067693546,-19.0486363886758,
6.49491484955768));
#162873=CARTESIAN_POINT('Ctrl Pts',(-16.6169513651074,-18.9992790637633,
6.49193194662284));
#162874=CARTESIAN_POINT('Ctrl Pts',(-16.6164273661252,-18.9498988449414,
6.488949043688));
#162875=CARTESIAN_POINT('Ctrl Pts',(-16.6176234550289,-18.9006256883613,
6.48596614075315));
#162876=CARTESIAN_POINT('Ctrl Pts',(-16.6193830456439,-18.8281389496101,
6.48157793182226));
#162877=CARTESIAN_POINT('Ctrl Pts',(-16.6248744285954,-18.7556012223724,
6.47718972289136));
#162878=CARTESIAN_POINT('Ctrl Pts',(-16.6341051990332,-18.6834281755797,
6.47280151396046));
#162879=CARTESIAN_POINT('Ctrl Pts',(-16.6433222694771,-18.6113622455548,
6.46841981785919));
#162880=CARTESIAN_POINT('Ctrl Pts',(-16.656267649465,-18.5396603960522,
6.46403812175793));
#162881=CARTESIAN_POINT('Ctrl Pts',(-16.6728969413429,-18.4687369436899,
6.45965642565666));
#162882=CARTESIAN_POINT('Ctrl Pts',(-16.6895066924793,-18.3978968320285,
6.45527987839702));
#162883=CARTESIAN_POINT('Ctrl Pts',(-16.709791646569,-18.3278337678025,
6.45090333113738));
#162884=CARTESIAN_POINT('Ctrl Pts',(-16.7336560032766,-18.2589539014086,
6.44652678387774));
#162885=CARTESIAN_POINT('Ctrl Pts',(-16.757505225556,-18.190117717625,6.44215301216076));
#162886=CARTESIAN_POINT('Ctrl Pts',(-16.7849291889405,-18.1224636975235,
6.43777924044379));
#162887=CARTESIAN_POINT('Ctrl Pts',(-16.815782089144,-18.0563834266432,
6.43340546872682));
#162888=CARTESIAN_POINT('Ctrl Pts',(-16.8466256007064,-17.9903232642113,
6.42903302796327));
#162889=CARTESIAN_POINT('Ctrl Pts',(-16.8808957735922,-17.9258363370627,
6.42466058719971));
#162890=CARTESIAN_POINT('Ctrl Pts',(-16.9183991025644,-17.8632932528771,
6.42028814643616));
#162891=CARTESIAN_POINT('Ctrl Pts',(-16.9559033905008,-17.8007485694579,
6.41591559386882));
#162892=CARTESIAN_POINT('Ctrl Pts',(-16.9966407488748,-17.7401482403576,
6.41154304130147));
#162893=CARTESIAN_POINT('Ctrl Pts',(-17.0403731142006,-17.6818358485229,
6.40717048873412));
#162894=CARTESIAN_POINT('Ctrl Pts',(-17.0841508666247,-17.6234629378885,
6.4027933981668));
#162895=CARTESIAN_POINT('Ctrl Pts',(-17.1309295419555,-17.5673830921179,
6.39841630759947));
#162896=CARTESIAN_POINT('Ctrl Pts',(-17.1804298596141,-17.5139079240531,
6.39403921703214));
#162897=CARTESIAN_POINT('Ctrl Pts',(-17.2299572112332,-17.4604035512143,
6.3896597359732));
#162898=CARTESIAN_POINT('Ctrl Pts',(-17.2822088187845,-17.4095070251029,
6.38528025491426));
#162899=CARTESIAN_POINT('Ctrl Pts',(-17.3368694420737,-17.3614921552823,
6.38090077385531));
#162900=CARTESIAN_POINT('Ctrl Pts',(-17.3916269509507,-17.3133921794274,
6.37651353019559));
#162901=CARTESIAN_POINT('Ctrl Pts',(-17.4488016237927,-17.2681843592166,
6.37212628653587));
#162902=CARTESIAN_POINT('Ctrl Pts',(-17.5080466246426,-17.226101010647,
6.36773904287615));
#162903=CARTESIAN_POINT('Ctrl Pts',(-17.5483275163857,-17.1974883887615,
6.36475613994134));
#162904=CARTESIAN_POINT('Ctrl Pts',(-17.5895648351148,-17.170319212664,
6.36177323700653));
#162905=CARTESIAN_POINT('Ctrl Pts',(-17.6316431823901,-17.1446543090297,
6.35879033407172));
#162906=CARTESIAN_POINT('Ctrl Pts',(-17.6935454914313,-17.1068981494094,
6.35440212514083));
#162907=CARTESIAN_POINT('Ctrl Pts',(-17.7575106221333,-17.0722522374745,
6.35001391620993));
#162908=CARTESIAN_POINT('Ctrl Pts',(-17.8231931738163,-17.0409479532527,
6.34562570727903));
#162909=CARTESIAN_POINT('Ctrl Pts',(-17.8887782417022,-17.009690129779,
6.34124401117776));
#162910=CARTESIAN_POINT('Ctrl Pts',(-17.9560752387291,-16.9817642944955,
6.33686231507649));
#162911=CARTESIAN_POINT('Ctrl Pts',(-18.0247117585802,-16.9573573777281,
6.33248061897523));
#162912=CARTESIAN_POINT('Ctrl Pts',(-18.093267625058,-16.9329791410304,
6.32810407171559));
#162913=CARTESIAN_POINT('Ctrl Pts',(-18.1631594352659,-16.9121117694419,
6.32372752445595));
#162914=CARTESIAN_POINT('Ctrl Pts',(-18.2339938260905,-16.8948945515476,
6.31935097719631));
#162915=CARTESIAN_POINT('Ctrl Pts',(-18.3047832947738,-16.8776882525628,
6.31497720547934));
#162916=CARTESIAN_POINT('Ctrl Pts',(-18.3765136904417,-16.8641276279119,
6.31060343376236));
#162917=CARTESIAN_POINT('Ctrl Pts',(-18.4487768305311,-16.8543020370897,
6.30622966204539));
#162918=CARTESIAN_POINT('Ctrl Pts',(-18.5210179807043,-16.8444794362278,
6.30185722128184));
#162919=CARTESIAN_POINT('Ctrl Pts',(-18.5937910757566,-16.838389677678,
6.29748478051829));
#162920=CARTESIAN_POINT('Ctrl Pts',(-18.6666797525648,-16.8360706570669,
6.29311233975473));
#162921=CARTESIAN_POINT('Ctrl Pts',(-18.7395702931445,-16.8337515771582,
6.28873978718739));
#162922=CARTESIAN_POINT('Ctrl Pts',(-18.8125759391505,-16.8352034399581,
6.28436723462004));
#162923=CARTESIAN_POINT('Ctrl Pts',(-18.8852789324484,-16.8404120466821,
6.2799946820527));
#162924=CARTESIAN_POINT('Ctrl Pts',(-18.958057379655,-16.8456260590946,
6.27561759148537));
#162925=CARTESIAN_POINT('Ctrl Pts',(-19.0305320648488,-16.8546045652848,
6.27124050091805));
#162926=CARTESIAN_POINT('Ctrl Pts',(-19.1022898016633,-16.8672814046038,
6.26686341035072));
#162927=CARTESIAN_POINT('Ctrl Pts',(-19.1740867280411,-16.8799651672152,
6.26248392929178));
#162928=CARTESIAN_POINT('Ctrl Pts',(-19.2451654560883,-16.8963511759145,
6.25810444823283));
#162929=CARTESIAN_POINT('Ctrl Pts',(-19.3151251217552,-16.9163225715097,
6.25372496717389));
#162930=CARTESIAN_POINT('Ctrl Pts',(-19.3852087904599,-16.9363293662695,
6.24933772351417));
#162931=CARTESIAN_POINT('Ctrl Pts',(-19.4541689789704,-16.9599340823955,
6.24495047985445));
#162932=CARTESIAN_POINT('Ctrl Pts',(-19.5216226105729,-16.9869708339787,
6.24056323619473));
#162933=CARTESIAN_POINT('Ctrl Pts',(-19.5674845802461,-17.0053532198001,
6.23758033325991));
#162934=CARTESIAN_POINT('Ctrl Pts',(-19.6126505362293,-17.0253211191867,
6.2345974303251));
#162935=CARTESIAN_POINT('Ctrl Pts',(-19.6570068699279,-17.0468104246386,
6.23161452739028));
#162936=CARTESIAN_POINT('Ctrl Pts',(-19.7222419452882,-17.0784148505164,
6.22722755755938));
#162937=CARTESIAN_POINT('Ctrl Pts',(-19.7859792078952,-17.1134353687254,
6.22284058772849));
#162938=CARTESIAN_POINT('Ctrl Pts',(-19.847837465415,-17.1517069403462,
6.21845361789759));
#162939=CARTESIAN_POINT('Ctrl Pts',(-19.9096117325667,-17.1899265473058,
6.21407260463944));
#162940=CARTESIAN_POINT('Ctrl Pts',(-19.9695116495773,-17.2313881992686,
6.2096915913813));
#162941=CARTESIAN_POINT('Ctrl Pts',(-20.0271786200073,-17.2758800589588,
6.20531057812316));
#162942=CARTESIAN_POINT('Ctrl Pts',(-20.0847863205803,-17.3203261901124,
6.20093406765105));
#162943=CARTESIAN_POINT('Ctrl Pts',(-20.1401652493144,-17.367796055159,
6.19655755717894));
#162944=CARTESIAN_POINT('Ctrl Pts',(-20.1929853613491,-17.4180343174083,
6.19218104670683));
#162945=CARTESIAN_POINT('Ctrl Pts',(-20.2457686121952,-17.4682375202457,
6.18780759043834));
#162946=CARTESIAN_POINT('Ctrl Pts',(-20.2959962435542,-17.521204952502,
6.18343413416985));
#162947=CARTESIAN_POINT('Ctrl Pts',(-20.3433722233308,-17.5766418478188,
6.17906067790137));
#162948=CARTESIAN_POINT('Ctrl Pts',(-20.3907430256997,-17.6320726848037,
6.17468769957901));
#162949=CARTESIAN_POINT('Ctrl Pts',(-20.4352624726777,-17.6899720904887,
6.17031472125666));
#162950=CARTESIAN_POINT('Ctrl Pts',(-20.4766732169276,-17.7500103748355,
6.1659417429343));
#162951=CARTESIAN_POINT('Ctrl Pts',(-20.5180810237586,-17.8100444004421,
6.16156907480366));
#162952=CARTESIAN_POINT('Ctrl Pts',(-20.5563802984018,-17.872216601689,
6.15719640667301));
#162953=CARTESIAN_POINT('Ctrl Pts',(-20.5913568209674,-17.9361680062108,
6.15282373854237));
#162954=CARTESIAN_POINT('Ctrl Pts',(-20.6263573793841,-18.0001633581098,
6.1484480655161));
#162955=CARTESIAN_POINT('Ctrl Pts',(-20.6580304037707,-18.0659399262137,
6.14407239248983));
#162956=CARTESIAN_POINT('Ctrl Pts',(-20.6862080122609,-18.1331148573429,
6.13969671946356));
#162957=CARTESIAN_POINT('Ctrl Pts',(-20.6990632498902,-18.1637615214382,
6.13770044229331));
#162958=CARTESIAN_POINT('Ctrl Pts',(-20.7111916196051,-18.1946989607123,
6.13570416512306));
#162959=CARTESIAN_POINT('Ctrl Pts',(-20.7225805737622,-18.2258896078036,
6.13370788795281));
#162960=CARTESIAN_POINT('Ctrl Pts',(-20.7193262654686,-18.2270707613317,
6.9336185967496));
#162961=CARTESIAN_POINT('Ctrl Pts',(-20.8041091853424,-18.460047360634,
6.91876474672015));
#162962=CARTESIAN_POINT('Ctrl Pts',(-20.8501556708863,-18.707244192998,
6.90391089669071));
#162963=CARTESIAN_POINT('Ctrl Pts',(-20.8523539331563,-18.9537405760439,
6.88905704666127));
#162964=CARTESIAN_POINT('Origin',(-18.734,-18.952,0.));
#162965=CARTESIAN_POINT('',(-20.7225806049454,-18.2258896932043,7.9573447159704));
#162966=CARTESIAN_POINT('',(-20.7225805631882,-18.2258895788448,7.73405224475123));
#162967=CARTESIAN_POINT('',(-20.7225805737622,-18.2258896078036,0.));
#162968=CARTESIAN_POINT('',(-20.8509992001554,-18.9539106864308,7.91072959189229));
#162969=CARTESIAN_POINT('Ctrl Pts',(-20.7225806049454,-18.2258896932043,
7.9573447159704));
#162970=CARTESIAN_POINT('Ctrl Pts',(-20.7291121646355,-18.2437775165808,
7.95624418976471));
#162971=CARTESIAN_POINT('Ctrl Pts',(-20.7354040725529,-18.2617581421778,
7.9551359376618));
#162972=CARTESIAN_POINT('Ctrl Pts',(-20.7459521244103,-18.2932600438301,
7.95318942672229));
#162973=CARTESIAN_POINT('Ctrl Pts',(-20.750315027364,-18.3067377458204,
7.95235510459761));
#162974=CARTESIAN_POINT('Ctrl Pts',(-20.7570545432907,-18.3282931851018,
7.95101787804382));
#162975=CARTESIAN_POINT('Ctrl Pts',(-20.7595188457556,-18.3363432137585,
7.9505178504801));
#162976=CARTESIAN_POINT('Ctrl Pts',(-20.763786514856,-18.350587230421,7.94963188454869));
#162977=CARTESIAN_POINT('Ctrl Pts',(-20.7656097187089,-18.3567751981563,
7.94924660042969));
#162978=CARTESIAN_POINT('Ctrl Pts',(-20.7693280461947,-18.3696113551058,
7.94844651352588));
#162979=CARTESIAN_POINT('Ctrl Pts',(-20.771218943158,-18.3762606794711,
7.94803157817029));
#162980=CARTESIAN_POINT('Ctrl Pts',(-20.7760009352766,-18.3933950639643,
7.94696106243246));
#162981=CARTESIAN_POINT('Ctrl Pts',(-20.7788438303318,-18.4038932614228,
7.94630392472707));
#162982=CARTESIAN_POINT('Ctrl Pts',(-20.7848191483326,-18.426652534329,
7.94487647843388));
#162983=CARTESIAN_POINT('Ctrl Pts',(-20.7879227668369,-18.4389206729892,
7.94410526548381));
#162984=CARTESIAN_POINT('Ctrl Pts',(-20.7966338678917,-18.4747005572732,
7.94185065864242));
#162985=CARTESIAN_POINT('Ctrl Pts',(-20.801948757875,-18.4982808240802,
7.94035804412167));
#162986=CARTESIAN_POINT('Ctrl Pts',(-20.8363442493001,-18.6640670291866,
7.92981464442311));
#162987=CARTESIAN_POINT('Ctrl Pts',(-20.851130049531,-18.8088169703404,
7.92031692626474));
#162988=CARTESIAN_POINT('Ctrl Pts',(-20.8509991383105,-18.9539100765585,
7.91072952400752));
#162989=CARTESIAN_POINT('Ctrl Pts',(-20.8509991377667,-18.9539106792569,
7.91072948418266));
#162990=CARTESIAN_POINT('Ctrl Pts',(-20.8508884779766,-19.0765197877048,
7.90262777016645));
#162991=CARTESIAN_POINT('Ctrl Pts',(-20.8401264221114,-19.198901967048,
7.89450607667186));
#162992=CARTESIAN_POINT('Ctrl Pts',(-20.8166444849761,-19.3320511155589,
7.88604145694026));
#162993=CARTESIAN_POINT('Ctrl Pts',(-20.8143518747477,-19.3444066702894,
7.88525971599234));
#162994=CARTESIAN_POINT('Ctrl Pts',(-20.8106712431876,-19.3633030964508,
7.88407060985964));
#162995=CARTESIAN_POINT('Ctrl Pts',(-20.8093620672279,-19.3698588063086,
7.88365927391941));
#162996=CARTESIAN_POINT('Ctrl Pts',(-20.8071513236229,-19.3806623897957,
7.88298350988733));
#162997=CARTESIAN_POINT('Ctrl Pts',(-20.8062677118098,-19.3849138325531,
7.88271812068513));
#162998=CARTESIAN_POINT('Ctrl Pts',(-20.8045210240075,-19.3931900179904,
7.88220258368105));
#162999=CARTESIAN_POINT('Ctrl Pts',(-20.8036592788117,-19.3972150189818,
7.88195236298181));
#163000=CARTESIAN_POINT('Ctrl Pts',(-20.8020280136667,-19.4047271656756,
7.88148633162137));
#163001=CARTESIAN_POINT('Ctrl Pts',(-20.8012614183712,-19.4082148399613,
7.88127036308551));
#163002=CARTESIAN_POINT('Ctrl Pts',(-20.7994932703404,-19.4161631715941,
7.88077906375489));
#163003=CARTESIAN_POINT('Ctrl Pts',(-20.7984860931884,-19.4206225257255,
7.88050405886988));
#163004=CARTESIAN_POINT('Ctrl Pts',(-20.7953527021961,-19.4342896849747,
7.87966306763098));
#163005=CARTESIAN_POINT('Ctrl Pts',(-20.7931792404429,-19.4434866898566,
7.87909972326578));
#163006=CARTESIAN_POINT('Ctrl Pts',(-20.7619486583876,-19.5717941388179,
7.87127271430771));
#163007=CARTESIAN_POINT('Ctrl Pts',(-20.7226548100719,-19.6881938883943,
7.86455357872539));
#163008=CARTESIAN_POINT('Ctrl Pts',(-20.6449227980636,-19.8658628497002,
7.85400328150231));
#163009=CARTESIAN_POINT('Ctrl Pts',(-20.6130671500829,-19.929690010207,
7.85014925697576));
#163010=CARTESIAN_POINT('Ctrl Pts',(-20.5342707230545,-20.069434682374,
7.84135941082986));
#163011=CARTESIAN_POINT('Ctrl Pts',(-20.4856322543038,-20.1442319974535,
7.83640110244062));
#163012=CARTESIAN_POINT('Ctrl Pts',(-20.4120584880257,-20.2431131116241,
7.82931016918979));
#163013=CARTESIAN_POINT('Ctrl Pts',(-20.3910310721284,-20.2699913462734,
7.827323909304));
#163014=CARTESIAN_POINT('Ctrl Pts',(-20.3624525905365,-20.3047563042614,
7.82467005732998));
#163015=CARTESIAN_POINT('Ctrl Pts',(-20.3554764305954,-20.3131104424966,
7.82402566957444));
#163016=CARTESIAN_POINT('Ctrl Pts',(-20.3439634281607,-20.3266834443802,
7.82296759052642));
#163017=CARTESIAN_POINT('Ctrl Pts',(-20.3394648312443,-20.3319345948855,
7.82255547151133));
#163018=CARTESIAN_POINT('Ctrl Pts',(-20.3307201304967,-20.3420415216623,
7.82175684321005));
#163019=CARTESIAN_POINT('Ctrl Pts',(-20.3264773960049,-20.3469001214652,
7.82137047621034));
#163020=CARTESIAN_POINT('Ctrl Pts',(-20.3166487568704,-20.3580521760454,
7.82047792666548));
#163021=CARTESIAN_POINT('Ctrl Pts',(-20.3110474281122,-20.364331836247,
7.81997110104062));
#163022=CARTESIAN_POINT('Ctrl Pts',(-20.2959253962986,-20.3810830457071,
7.81860760903631));
#163023=CARTESIAN_POINT('Ctrl Pts',(-20.2863370023308,-20.3914926575209,
7.81774808586631));
#163024=CARTESIAN_POINT('Ctrl Pts',(-20.2021849914205,-20.4810334416281,
7.81024647268885));
#163025=CARTESIAN_POINT('Ctrl Pts',(-20.1217436847516,-20.5543955644701,
7.80334484366058));
#163026=CARTESIAN_POINT('Ctrl Pts',(-19.959008586461,-20.6813311267264,
7.78990636276258));
#163027=CARTESIAN_POINT('Ctrl Pts',(-19.8779167312633,-20.7360082007562,
7.78342171273805));
#163028=CARTESIAN_POINT('Ctrl Pts',(-19.7310914805351,-20.8208679833736,
7.77224413309551));
#163029=CARTESIAN_POINT('Ctrl Pts',(-19.6670415366176,-20.8536555642205,
7.76753910418112));
#163030=CARTESIAN_POINT('Ctrl Pts',(-19.5707324088792,-20.8969167935079,
7.76082280057584));
#163031=CARTESIAN_POINT('Ctrl Pts',(-19.539694813602,-20.9099781973353,
7.75871088613623));
#163032=CARTESIAN_POINT('Ctrl Pts',(-19.5015761335029,-20.924959442176,
7.75619173333209));
#163033=CARTESIAN_POINT('Ctrl Pts',(-19.4947815122547,-20.9275894247936,
7.75574554216904));
#163034=CARTESIAN_POINT('Ctrl Pts',(-19.4840931107764,-20.9316632462458,
7.75504826522288));
#163035=CARTESIAN_POINT('Ctrl Pts',(-19.4802085035831,-20.9331307663138,
7.75479579832622));
#163036=CARTESIAN_POINT('Ctrl Pts',(-19.4729794620856,-20.9358374618164,
7.75432777358358));
#163037=CARTESIAN_POINT('Ctrl Pts',(-19.4696362468064,-20.9370796036796,
7.75411204444848));
#163038=CARTESIAN_POINT('Ctrl Pts',(-19.462049190355,-20.9398767073513,
7.75362408416469));
#163039=CARTESIAN_POINT('Ctrl Pts',(-19.4578035097067,-20.9414265272718,
7.75335216142913));
#163040=CARTESIAN_POINT('Ctrl Pts',(-19.4451919437508,-20.9459844670143,
7.75254770962068));
#163041=CARTESIAN_POINT('Ctrl Pts',(-19.4368119173993,-20.9489535424173,
7.75201744651799));
#163042=CARTESIAN_POINT('Ctrl Pts',(-19.3737829734597,-20.9708390347424,
7.74805940055269));
#163043=CARTESIAN_POINT('Ctrl Pts',(-19.3183930075901,-20.9875636520926,
7.74475096310306));
#163044=CARTESIAN_POINT('Ctrl Pts',(-19.1043534426584,-21.0427318428755,
7.73236527602057));
#163045=CARTESIAN_POINT('Ctrl Pts',(-18.9421390479485,-21.0650560415417,
7.72375961938505));
#163046=CARTESIAN_POINT('Ctrl Pts',(-18.7189084647188,-21.0697982257335,
7.71139187355725));
#163047=CARTESIAN_POINT('Ctrl Pts',(-18.6588315277271,-21.0685174176337,
7.70801705079311));
#163048=CARTESIAN_POINT('Ctrl Pts',(-18.5747507198067,-21.0631404303624,
7.70317892672398));
#163049=CARTESIAN_POINT('Ctrl Pts',(-18.5506370702587,-21.0611828319601,
7.70177822887931));
#163050=CARTESIAN_POINT('Ctrl Pts',(-18.5085811162129,-21.0570419965381,
7.69930932516665));
#163051=CARTESIAN_POINT('Ctrl Pts',(-18.4906231345173,-21.0550414051365,
7.69824679318016));
#163052=CARTESIAN_POINT('Ctrl Pts',(-18.464222180628,-21.0517575572766,
7.69667162738966));
#163053=CARTESIAN_POINT('Ctrl Pts',(-18.455757545468,-21.0506526640692,
7.69616461529144));
#163054=CARTESIAN_POINT('Ctrl Pts',(-18.4409127674991,-21.0486235790028,
7.69527187180842));
#163055=CARTESIAN_POINT('Ctrl Pts',(-18.4345296936801,-21.0477213774973,
7.69488684032161));
#163056=CARTESIAN_POINT('Ctrl Pts',(-18.4221316798874,-21.0459112097219,
7.69413668400826));
#163057=CARTESIAN_POINT('Ctrl Pts',(-18.4161163309557,-21.0450064440997,
7.69377166416281));
#163058=CARTESIAN_POINT('Ctrl Pts',(-18.4017269415461,-21.0427786801006,
7.69289593507089));
#163059=CARTESIAN_POINT('Ctrl Pts',(-18.3933568340568,-21.0414312873992,
7.69238445609245));
#163060=CARTESIAN_POINT('Ctrl Pts',(-18.3630705634205,-21.0363690818403,
7.69052606040096));
#163061=CARTESIAN_POINT('Ctrl Pts',(-18.341205753932,-21.0323595211849,
7.68916982520187));
#163062=CARTESIAN_POINT('Ctrl Pts',(-18.1386054449318,-20.9918989973368,
7.67646273917391));
#163063=CARTESIAN_POINT('Ctrl Pts',(-17.9633259877772,-20.9323325699457,
7.66432453444339));
#163064=CARTESIAN_POINT('Ctrl Pts',(-17.7253994061342,-20.8150535475416,
7.64680939966994));
#163065=CARTESIAN_POINT('Ctrl Pts',(-17.6548893923708,-20.7751197761543,
7.64148800580103));
#163066=CARTESIAN_POINT('Ctrl Pts',(-17.5563713087634,-20.7116004093602,
7.6340142357973));
#163067=CARTESIAN_POINT('Ctrl Pts',(-17.5264136361062,-20.6911775277672,
7.63173652456848));
#163068=CARTESIAN_POINT('Ctrl Pts',(-17.4909235300947,-20.6656235970081,
7.62904591514725));
#163069=CARTESIAN_POINT('Ctrl Pts',(-17.4848768797669,-20.6612209853006,
7.62858778168012));
#163070=CARTESIAN_POINT('Ctrl Pts',(-17.4755018529827,-20.654318635762,
7.62787807216377));
#163071=CARTESIAN_POINT('Ctrl Pts',(-17.4721573705127,-20.6518410228035,
7.62762500822957));
#163072=CARTESIAN_POINT('Ctrl Pts',(-17.4659614145795,-20.6472226576754,
7.62715644275172));
#163073=CARTESIAN_POINT('Ctrl Pts',(-17.4631080690923,-20.645084585437,
7.62694076638013));
#163074=CARTESIAN_POINT('Ctrl Pts',(-17.4566605511869,-20.6402278403329,
7.62645364408698));
#163075=CARTESIAN_POINT('Ctrl Pts',(-17.4530696591624,-20.6375049009582,
7.62618250213815));
#163076=CARTESIAN_POINT('Ctrl Pts',(-17.4422363136442,-20.6292354617392,
7.62536487854274));
#163077=CARTESIAN_POINT('Ctrl Pts',(-17.4350208804146,-20.6236535134842,
7.62482082970714));
#163078=CARTESIAN_POINT('Ctrl Pts',(-17.3795366093111,-20.580154018043,
7.62063936766184));
#163079=CARTESIAN_POINT('Ctrl Pts',(-17.3328966002781,-20.5401962516233,
7.61713648515878));
#163080=CARTESIAN_POINT('Ctrl Pts',(-17.1808017341162,-20.3979690574869,
7.60549960097017));
#163081=CARTESIAN_POINT('Ctrl Pts',(-17.0842703882613,-20.2867839309853,
7.5977131546074));
#163082=CARTESIAN_POINT('Ctrl Pts',(-16.9468070252436,-20.0905227558134,
7.58451580236484));
#163083=CARTESIAN_POINT('Ctrl Pts',(-16.8986499810703,-20.0111412667951,
7.57930739245145));
#163084=CARTESIAN_POINT('Ctrl Pts',(-16.8461310462591,-19.9101669778376,
7.57267773953802));
#163085=CARTESIAN_POINT('Ctrl Pts',(-16.8366863769089,-19.8913264141453,
7.57144086081967));
#163086=CARTESIAN_POINT('Ctrl Pts',(-16.8236312438081,-19.8642830841738,
7.56966433344511));
#163087=CARTESIAN_POINT('Ctrl Pts',(-16.8197889539165,-19.8561931638766,
7.56913275068293));
#163088=CARTESIAN_POINT('Ctrl Pts',(-16.813239783298,-19.8421750711511,
7.56821128690155));
#163089=CARTESIAN_POINT('Ctrl Pts',(-16.8105087096375,-19.8362582890758,
7.56782224848084));
#163090=CARTESIAN_POINT('Ctrl Pts',(-16.8053255422307,-19.8248914885335,
7.56707462125713));
#163091=CARTESIAN_POINT('Ctrl Pts',(-16.8028691187331,-19.8194435042612,
7.5667161862044));
#163092=CARTESIAN_POINT('Ctrl Pts',(-16.7965279868229,-19.8052193794704,
7.5657800376019));
#163093=CARTESIAN_POINT('Ctrl Pts',(-16.7926798648345,-19.7964271664299,
7.56520107726022));
#163094=CARTESIAN_POINT('Ctrl Pts',(-16.7796940204716,-19.7661990724295,
7.56320934949621));
#163095=CARTESIAN_POINT('Ctrl Pts',(-16.7708507582233,-19.744639248073,
7.56178663902572));
#163096=CARTESIAN_POINT('Ctrl Pts',(-16.7001129760838,-19.563731100552,
7.54982680060326));
#163097=CARTESIAN_POINT('Ctrl Pts',(-16.6573844864417,-19.3975980731648,
7.53862641072276));
#163098=CARTESIAN_POINT('Ctrl Pts',(-16.6233204444518,-19.13871544722,7.521371556759));
#163099=CARTESIAN_POINT('Ctrl Pts',(-16.6172799776276,-19.0485877072119,
7.51541663743598));
#163100=CARTESIAN_POINT('Ctrl Pts',(-16.6168937408165,-18.9197188059379,
7.50718327515759));
#163101=CARTESIAN_POINT('Ctrl Pts',(-16.6178351330105,-18.881093874975,
7.50475228711868));
#163102=CARTESIAN_POINT('Ctrl Pts',(-16.6202270189575,-18.8349068592937,
7.50190606007237));
#163103=CARTESIAN_POINT('Ctrl Pts',(-16.620662011859,-18.8273020813545,
7.50143940052899));
#163104=CARTESIAN_POINT('Ctrl Pts',(-16.6214000285952,-18.8155158094416,
7.50071938696682));
#163105=CARTESIAN_POINT('Ctrl Pts',(-16.6216744382275,-18.8113326788562,
7.50046447600715));
#163106=CARTESIAN_POINT('Ctrl Pts',(-16.6222050581317,-18.803595761432,
7.49999421090593));
#163107=CARTESIAN_POINT('Ctrl Pts',(-16.6224578121275,-18.8000418357937,
7.49977867105326));
#163108=CARTESIAN_POINT('Ctrl Pts',(-16.6230477069762,-18.7920332106285,
7.49929401966149));
#163109=CARTESIAN_POINT('Ctrl Pts',(-16.6233899758371,-18.7875789433532,
7.49902519886856));
#163110=CARTESIAN_POINT('Ctrl Pts',(-16.6244360954273,-18.7745066269026,
7.49823833715701));
#163111=CARTESIAN_POINT('Ctrl Pts',(-16.6251786580974,-18.7658916479788,
7.4977224174996));
#163112=CARTESIAN_POINT('Ctrl Pts',(-16.6307248349171,-18.7058487007593,
7.49414359651874));
#163113=CARTESIAN_POINT('Ctrl Pts',(-16.637356826807,-18.6546025879785,
7.49117567375488));
#163114=CARTESIAN_POINT('Ctrl Pts',(-16.6494413839244,-18.5821639457779,
7.48703966121493));
#163115=CARTESIAN_POINT('Ctrl Pts',(-16.6533565355493,-18.5607377479435,
7.48582376604037));
#163116=CARTESIAN_POINT('Ctrl Pts',(-16.6665994321883,-18.4940972211443,
7.48205523119524));
#163117=CARTESIAN_POINT('Ctrl Pts',(-16.6770760202979,-18.4491242202059,
7.47953085785205));
#163118=CARTESIAN_POINT('Ctrl Pts',(-16.7172948733586,-18.2988936293448,
7.47106361971575));
#163119=CARTESIAN_POINT('Ctrl Pts',(-16.7537170913693,-18.1956097449709,
7.46517527766237));
#163120=CARTESIAN_POINT('Ctrl Pts',(-16.8202493175692,-18.0452006129496,
7.45603035582364));
#163121=CARTESIAN_POINT('Ctrl Pts',(-16.8445041760552,-17.995688498136,
7.45292250372553));
#163122=CARTESIAN_POINT('Ctrl Pts',(-16.8869471288455,-17.9169821750941,
7.4477779865052));
#163123=CARTESIAN_POINT('Ctrl Pts',(-16.9039633479972,-17.8871845876408,
7.44578071920798));
#163124=CARTESIAN_POINT('Ctrl Pts',(-16.9272822671727,-17.8485613413166,
7.44311989438058));
#163125=CARTESIAN_POINT('Ctrl Pts',(-16.9329398000158,-17.8393509137813,
7.44247986918972));
#163126=CARTESIAN_POINT('Ctrl Pts',(-16.9423229786939,-17.8243342529338,
7.44142713928122));
#163127=CARTESIAN_POINT('Ctrl Pts',(-16.946006953364,-17.8185021176764,
7.44101597598107));
#163128=CARTESIAN_POINT('Ctrl Pts',(-16.953194210017,-17.8072461274672,
7.44021790521636));
#163129=CARTESIAN_POINT('Ctrl Pts',(-16.9566939348938,-17.8018200837174,
7.43983113315872));
#163130=CARTESIAN_POINT('Ctrl Pts',(-16.9648334160641,-17.7893263236327,
7.43893576594251));
#163131=CARTESIAN_POINT('Ctrl Pts',(-16.969490774961,-17.7822702573048,
7.43842651470706));
#163132=CARTESIAN_POINT('Ctrl Pts',(-16.9821331243412,-17.7633639598381,
7.43705224776383));
#163133=CARTESIAN_POINT('Ctrl Pts',(-16.9901959294063,-17.7515665225978,
7.43618430426384));
#163134=CARTESIAN_POINT('Ctrl Pts',(-17.0652574986312,-17.644089103529,
7.42817971778301));
#163135=CARTESIAN_POINT('Ctrl Pts',(-17.1399371276725,-17.5540414135516,
7.42074153172824));
#163136=CARTESIAN_POINT('Ctrl Pts',(-17.3354199595754,-17.3544713981144,
7.40249421335316));
#163137=CARTESIAN_POINT('Ctrl Pts',(-17.462189503704,-17.2518171049488,
7.39154536572418));
#163138=CARTESIAN_POINT('Ctrl Pts',(-17.6270394328668,-17.1471746298091,
7.37913638044254));
#163139=CARTESIAN_POINT('Ctrl Pts',(-17.6550249036619,-17.1303059181342,
7.37708855267636));
#163140=CARTESIAN_POINT('Ctrl Pts',(-17.6896861162014,-17.1104924425565,
7.37463342060822));
#163141=CARTESIAN_POINT('Ctrl Pts',(-17.695999445713,-17.1069264446045,
7.37418946343051));
#163142=CARTESIAN_POINT('Ctrl Pts',(-17.7059218426768,-17.1013889625903,
7.37349691308908));
#163143=CARTESIAN_POINT('Ctrl Pts',(-17.7095184758355,-17.0993954775349,
7.37324694390315));
#163144=CARTESIAN_POINT('Ctrl Pts',(-17.7162497599066,-17.0956901646851,
7.37278113149526));
#163145=CARTESIAN_POINT('Ctrl Pts',(-17.7193828999214,-17.0939758084574,
7.37256513191096));
#163146=CARTESIAN_POINT('Ctrl Pts',(-17.726541819582,-17.0900821795917,
7.37207343934817));
#163147=CARTESIAN_POINT('Ctrl Pts',(-17.7305703306298,-17.0879080347859,
7.3717980743213));
#163148=CARTESIAN_POINT('Ctrl Pts',(-17.7429638487952,-17.0812712022994,
7.37095488597408));
#163149=CARTESIAN_POINT('Ctrl Pts',(-17.7513519404872,-17.0768515562118,
7.37038972475761));
#163150=CARTESIAN_POINT('Ctrl Pts',(-17.8671859526874,-17.0168098893848,
7.36265700851703));
#163151=CARTESIAN_POINT('Ctrl Pts',(-17.9791944820619,-16.9704338124156,
7.35601949980941));
#163152=CARTESIAN_POINT('Ctrl Pts',(-18.2651924850981,-16.8798164794217,
7.33969354614841));
#163153=CARTESIAN_POINT('Ctrl Pts',(-18.4419637838506,-16.8476158030409,
7.33007486661242));
#163154=CARTESIAN_POINT('Ctrl Pts',(-18.6421236366903,-16.836885544938,
7.31840391301656));
#163155=CARTESIAN_POINT('Ctrl Pts',(-18.6635892708165,-16.8360622165588,
7.31714355834492));
#163156=CARTESIAN_POINT('Ctrl Pts',(-18.6940855953224,-16.8353570711439,
7.31533916911888));
#163157=CARTESIAN_POINT('Ctrl Pts',(-18.7031091702568,-16.8352061506196,
7.31480355573699));
#163158=CARTESIAN_POINT('Ctrl Pts',(-18.7186621466533,-16.8350454940509,
7.31387732129739));
#163159=CARTESIAN_POINT('Ctrl Pts',(-18.7251911837587,-16.835008258569,
7.31348756669342));
#163160=CARTESIAN_POINT('Ctrl Pts',(-18.7376819741543,-16.8349948074066,
7.31274010795831));
#163161=CARTESIAN_POINT('Ctrl Pts',(-18.7436436680062,-16.8350135709129,
7.31238256501264));
#163162=CARTESIAN_POINT('Ctrl Pts',(-18.7591228076153,-16.8351276762284,
7.31145213909697));
#163163=CARTESIAN_POINT('Ctrl Pts',(-18.7686397535281,-16.8352620205938,
7.31087803919449));
#163164=CARTESIAN_POINT('Ctrl Pts',(-18.8009696861401,-16.8359364892325,
7.30892062634389));
#163165=CARTESIAN_POINT('Ctrl Pts',(-18.8237740984467,-16.8367812718875,
7.30752782698009));
#163166=CARTESIAN_POINT('Ctrl Pts',(-19.0240757247027,-16.8474462844111,
7.29518352548989));
#163167=CARTESIAN_POINT('Ctrl Pts',(-19.1996626216888,-16.8792182317456,
7.28350747807423));
#163168=CARTESIAN_POINT('Ctrl Pts',(-19.4506665025062,-16.9581655027858,
7.26612453331546));
#163169=CARTESIAN_POINT('Ctrl Pts',(-19.5305375617882,-16.9887076973626,
7.26049822828394));
#163170=CARTESIAN_POINT('Ctrl Pts',(-19.6424270576734,-17.0394494875494,
7.25265703056099));
#163171=CARTESIAN_POINT('Ctrl Pts',(-19.6760922428569,-17.0558059736017,
7.25030390775852));
#163172=CARTESIAN_POINT('Ctrl Pts',(-19.7160080830397,-17.0765250988076,
7.24753660367672));
#163173=CARTESIAN_POINT('Ctrl Pts',(-19.7226892734233,-17.0800385942231,
7.24707418989989));
#163174=CARTESIAN_POINT('Ctrl Pts',(-19.7330383415198,-17.0855518112681,
7.24635930592242));
#163175=CARTESIAN_POINT('Ctrl Pts',(-19.7367192564454,-17.0875267385943,
7.24610531333593));
#163176=CARTESIAN_POINT('Ctrl Pts',(-19.7435300020198,-17.091206922238,
7.24563589824954));
#163177=CARTESIAN_POINT('Ctrl Pts',(-19.7466613441442,-17.0929091723117,
7.24542029543805));
#163178=CARTESIAN_POINT('Ctrl Pts',(-19.753724749806,-17.0967720993383,
7.2449344378523));
#163179=CARTESIAN_POINT('Ctrl Pts',(-19.7576542416068,-17.0989373666136,
7.24466448030701));
#163180=CARTESIAN_POINT('Ctrl Pts',(-19.7692143279946,-17.1053553116191,
7.24387119334701));
#163181=CARTESIAN_POINT('Ctrl Pts',(-19.7768256250847,-17.1096428056355,
7.24335003750475));
#163182=CARTESIAN_POINT('Ctrl Pts',(-19.8310962424684,-17.140657884197,
7.23964075177672));
#163183=CARTESIAN_POINT('Ctrl Pts',(-19.8767530093681,-17.1691099228594,
7.2365556509409));
#163184=CARTESIAN_POINT('Ctrl Pts',(-20.0608279427225,-17.2938004730959,
7.22405657322377));
#163185=CARTESIAN_POINT('Ctrl Pts',(-20.1885933942022,-17.4046590965979,
7.21518670302042));
#163186=CARTESIAN_POINT('Ctrl Pts',(-20.3564534555601,-17.5896733212733,
7.20134232228929));
#163187=CARTESIAN_POINT('Ctrl Pts',(-20.407528852064,-17.6529279118329,
7.19675121411317));
#163188=CARTESIAN_POINT('Ctrl Pts',(-20.4662740091775,-17.7349128619316,
7.19086736104466));
#163189=CARTESIAN_POINT('Ctrl Pts',(-20.4774847979088,-17.7510274500799,
7.18971407501103));
#163190=CARTESIAN_POINT('Ctrl Pts',(-20.4933402539565,-17.7745083341693,
7.18803712681663));
#163191=CARTESIAN_POINT('Ctrl Pts',(-20.4981663211925,-17.7817513341116,
7.18752032732416));
#163192=CARTESIAN_POINT('Ctrl Pts',(-20.5065035597332,-17.794432709391,
7.18661622670279));
#163193=CARTESIAN_POINT('Ctrl Pts',(-20.5100347288258,-17.7998578463907,
7.18622968179366));
#163194=CARTESIAN_POINT('Ctrl Pts',(-20.5168105233643,-17.8103730584787,
7.1854808746197));
#163195=CARTESIAN_POINT('Ctrl Pts',(-20.52005837287,-17.8154609890754,7.18511873755079));
#163196=CARTESIAN_POINT('Ctrl Pts',(-20.5277198372757,-17.8275770282756,
7.18425676978858));
#163197=CARTESIAN_POINT('Ctrl Pts',(-20.5321139475799,-17.8346172981343,
7.18375622322555));
#163198=CARTESIAN_POINT('Ctrl Pts',(-20.547545602996,-17.8596687434147,
7.18197612587293));
#163199=CARTESIAN_POINT('Ctrl Pts',(-20.5583545566611,-17.8778186237432,
7.18068824496313));
#163200=CARTESIAN_POINT('Ctrl Pts',(-20.6295618646363,-18.0015622251531,
7.17191704123909));
#163201=CARTESIAN_POINT('Ctrl Pts',(-20.6809596360427,-18.1119033527847,
7.1641218929178));
#163202=CARTESIAN_POINT('Ctrl Pts',(-20.722580619343,-18.2258897326345,
7.15616144973347));
#163203=CARTESIAN_POINT('',(-20.847808864184,-18.9524614626978,7.68893960118917));
#163204=CARTESIAN_POINT('Ctrl Pts',(-20.8476070359586,-18.9524685808987,
7.68905589349203));
#163205=CARTESIAN_POINT('Ctrl Pts',(-20.848239885686,-19.2779557825456,
7.66955339595671));
#163206=CARTESIAN_POINT('Ctrl Pts',(-20.6243346437841,-20.3101167079764,
7.6076589628609));
#163207=CARTESIAN_POINT('Ctrl Pts',(-19.0148744683191,-21.4394564387197,
7.50337259420462));
#163208=CARTESIAN_POINT('Ctrl Pts',(-16.794474806048,-20.5345839704445,
7.3761967875232));
#163209=CARTESIAN_POINT('Ctrl Pts',(-16.3534691287178,-18.1777889355253,
7.24902098084176));
#163210=CARTESIAN_POINT('Ctrl Pts',(-18.0964527733798,-16.5312844993037,
7.12184517416032));
#163211=CARTESIAN_POINT('Ctrl Pts',(-20.0208838101815,-17.0060915880697,
7.01671104612961));
#163212=CARTESIAN_POINT('Ctrl Pts',(-20.6031709119695,-17.9078852545191,
6.95396885365936));
#163213=CARTESIAN_POINT('Ctrl Pts',(-20.7193262654686,-18.2270707613317,
6.9336185967496));
#163214=CARTESIAN_POINT('Ctrl Pts',(-20.8509999712464,-18.9523489167874,
7.68710090301811));
#163215=CARTESIAN_POINT('Ctrl Pts',(-20.8510014360976,-18.9434611529801,
7.6876214684987));
#163216=CARTESIAN_POINT('Ctrl Pts',(-20.8509469309248,-18.9345735478661,
7.68814372234433));
#163217=CARTESIAN_POINT('Ctrl Pts',(-20.8507292584211,-18.9170624111266,
7.68917619302368));
#163218=CARTESIAN_POINT('Ctrl Pts',(-20.8505693532622,-18.9084390302998,
7.68968629804239));
#163219=CARTESIAN_POINT('Ctrl Pts',(-20.8502036146338,-18.893605983878,
7.69056668727183));
#163220=CARTESIAN_POINT('Ctrl Pts',(-20.8500231309564,-18.8873957609257,
7.69093617673417));
#163221=CARTESIAN_POINT('Ctrl Pts',(-20.8496088606408,-18.875017907279,
7.69167443940697));
#163222=CARTESIAN_POINT('Ctrl Pts',(-20.8493754333924,-18.8688503254636,
7.69204319777663));
#163223=CARTESIAN_POINT('Ctrl Pts',(-20.8488557235133,-18.8565429563131,
7.69278088374308));
#163224=CARTESIAN_POINT('Ctrl Pts',(-20.8485696657796,-18.8504032195806,
7.69314980073961));
#163225=CARTESIAN_POINT('Ctrl Pts',(-20.8477228782773,-18.8337853696163,
7.69415081943603));
#163226=CARTESIAN_POINT('Ctrl Pts',(-20.8471109811632,-18.8233101399852,
7.69478452060767));
#163227=CARTESIAN_POINT('Ctrl Pts',(-20.844514726168,-18.7838994926352,
7.69717908560958));
#163228=CARTESIAN_POINT('Ctrl Pts',(-20.8420137566289,-18.7550023837778,
7.69895605267754));
#163229=CARTESIAN_POINT('Ctrl Pts',(-20.8205675150906,-18.5551086828724,
7.71140108946184));
#163230=CARTESIAN_POINT('Ctrl Pts',(-20.7814502050678,-18.3871144038753,
7.72271554281783));
#163231=CARTESIAN_POINT('Ctrl Pts',(-20.722580563188,-18.2258895788442,
7.73405224475127));
#163232=CARTESIAN_POINT('Origin',(-18.734,-18.952,0.));
#163233=CARTESIAN_POINT('',(-20.7225806939367,-18.2258899369226,8.75434681593714));
#163234=CARTESIAN_POINT('',(-20.7225805426339,-18.2258895225534,8.53521110136663));
#163235=CARTESIAN_POINT('',(-20.7225805737622,-18.2258896078036,0.));
#163236=CARTESIAN_POINT('Ctrl Pts',(-20.7225806939367,-18.2258899369226,
8.75434681593714));
#163237=CARTESIAN_POINT('Ctrl Pts',(-20.7522189871416,-18.3070596392385,
8.74958609388981));
#163238=CARTESIAN_POINT('Ctrl Pts',(-20.7768869532507,-18.3900423068481,
8.74492446735276));
#163239=CARTESIAN_POINT('Ctrl Pts',(-20.8270296777673,-18.6065650054646,
8.732822301103));
#163240=CARTESIAN_POINT('Ctrl Pts',(-20.8448588566228,-18.741366397787,
8.7253255891255));
#163241=CARTESIAN_POINT('Ctrl Pts',(-20.8502665616911,-18.8937846453747,
8.71640102340825));
#163242=CARTESIAN_POINT('Ctrl Pts',(-20.8506630232942,-18.9106380729111,
8.715408521791));
#163243=CARTESIAN_POINT('Ctrl Pts',(-20.85095289411,-18.9356775534054,8.71392483201408));
#163244=CARTESIAN_POINT('Ctrl Pts',(-20.8510001744647,-18.9438614137362,
8.71343846151186));
#163245=CARTESIAN_POINT('Ctrl Pts',(-20.8509998627386,-18.9584435228824,
8.71256918852936));
#163246=CARTESIAN_POINT('Ctrl Pts',(-20.8509707194805,-18.964841701459,
8.71218686888589));
#163247=CARTESIAN_POINT('Ctrl Pts',(-20.8508481156784,-18.9783316693246,
8.71137882529349));
#163248=CARTESIAN_POINT('Ctrl Pts',(-20.8507480205219,-18.9854233058149,
8.71095289800032));
#163249=CARTESIAN_POINT('Ctrl Pts',(-20.8503886243636,-19.0041994779993,
8.70982210808948));
#163250=CARTESIAN_POINT('Ctrl Pts',(-20.8500681972762,-19.0158824759358,
8.70911533896458));
#163251=CARTESIAN_POINT('Ctrl Pts',(-20.8481220039195,-19.0703736722614,
8.70580369479496));
#163252=CARTESIAN_POINT('Ctrl Pts',(-20.8452939285419,-19.1131263546401,
8.70316145119592));
#163253=CARTESIAN_POINT('Ctrl Pts',(-20.833902049344,-19.2309338723355,
8.69575366709832));
#163254=CARTESIAN_POINT('Ctrl Pts',(-20.8226163014332,-19.3056562166429,
8.69090985328829));
#163255=CARTESIAN_POINT('Ctrl Pts',(-20.7814378526798,-19.5053193232467,
8.67762194617872));
#163256=CARTESIAN_POINT('Ctrl Pts',(-20.7441342285476,-19.6284041476841,
8.66904368299812));
#163257=CARTESIAN_POINT('Ctrl Pts',(-20.6896737654832,-19.7627435099994,
8.65959203219377));
#163258=CARTESIAN_POINT('Ctrl Pts',(-20.6832520940452,-19.7780636842366,
8.65851314531125));
#163259=CARTESIAN_POINT('Ctrl Pts',(-20.6554927754829,-19.8421623554157,
8.65399900269732));
#163260=CARTESIAN_POINT('Ctrl Pts',(-20.6324974129129,-19.8902068586563,
8.65061476691844));
#163261=CARTESIAN_POINT('Ctrl Pts',(-20.603657118634,-19.9450494385956,
8.64679243768987));
#163262=CARTESIAN_POINT('Ctrl Pts',(-20.5995537479213,-19.9527368027445,
8.64625762188909));
#163263=CARTESIAN_POINT('Ctrl Pts',(-20.5932681131467,-19.9643394539449,
8.6454521361562));
#163264=CARTESIAN_POINT('Ctrl Pts',(-20.5911207462444,-19.9682733988946,
8.64517933304397));
#163265=CARTESIAN_POINT('Ctrl Pts',(-20.5872434438664,-19.9753232327005,
8.6446910388086));
#163266=CARTESIAN_POINT('Ctrl Pts',(-20.585518126769,-19.978441585112,8.64447526001744));
#163267=CARTESIAN_POINT('Ctrl Pts',(-20.5817516576964,-19.9852087352868,
8.64400745508561));
#163268=CARTESIAN_POINT('Ctrl Pts',(-20.5797075756509,-19.9888558362048,
8.64375562032802));
#163269=CARTESIAN_POINT('Ctrl Pts',(-20.5739344548287,-19.9990852081065,
8.64305000892254));
#163270=CARTESIAN_POINT('Ctrl Pts',(-20.5701808751074,-20.0056536569985,
8.64259778047612));
#163271=CARTESIAN_POINT('Ctrl Pts',(-20.5475081043533,-20.0448399703605,
8.63990413633165));
#163272=CARTESIAN_POINT('Ctrl Pts',(-20.5277541350204,-20.0769699304541,
8.63771333291994));
#163273=CARTESIAN_POINT('Ctrl Pts',(-20.4598646273692,-20.1810532858221,
8.63061755555147));
#163274=CARTESIAN_POINT('Ctrl Pts',(-20.4081727363313,-20.2505871977334,
8.62587700674518));
#163275=CARTESIAN_POINT('Ctrl Pts',(-20.2388246733254,-20.4514033768187,
8.61158238343243));
#163276=CARTESIAN_POINT('Ctrl Pts',(-20.1089423701453,-20.5713315264266,
8.60211688859373));
#163277=CARTESIAN_POINT('Ctrl Pts',(-19.9470527619602,-20.6871422186922,
8.59054994190412));
#163278=CARTESIAN_POINT('Ctrl Pts',(-19.9281750744294,-20.700188020047,
8.58920559275252));
#163279=CARTESIAN_POINT('Ctrl Pts',(-19.9011552411323,-20.7182187381118,
8.58728589835375));
#163280=CARTESIAN_POINT('Ctrl Pts',(-19.8931852993571,-20.7234596876553,
8.58672019848798));
#163281=CARTESIAN_POINT('Ctrl Pts',(-19.8801738798225,-20.7318904529672,
8.58579742244521));
#163282=CARTESIAN_POINT('Ctrl Pts',(-19.8751538022231,-20.7351131724882,
8.58544157932636));
#163283=CARTESIAN_POINT('Ctrl Pts',(-19.8646137476526,-20.7418167895161,
8.58469480712144));
#163284=CARTESIAN_POINT('Ctrl Pts',(-19.8590911702102,-20.74529346278,8.5843037264495));
#163285=CARTESIAN_POINT('Ctrl Pts',(-19.8459086037695,-20.753507528335,
8.58337063104969));
#163286=CARTESIAN_POINT('Ctrl Pts',(-19.8382343304543,-20.7582216523207,
8.58282776661781));
#163287=CARTESIAN_POINT('Ctrl Pts',(-19.8122484270134,-20.7739566687607,
8.5809905649218));
#163288=CARTESIAN_POINT('Ctrl Pts',(-19.7938005161747,-20.7847489153051,
8.57968793716397));
#163289=CARTESIAN_POINT('Ctrl Pts',(-19.6922726404434,-20.8420984583779,
8.57252551833946));
#163290=CARTESIAN_POINT('Ctrl Pts',(-19.6062974776821,-20.883282350232,
8.5664766973249));
#163291=CARTESIAN_POINT('Ctrl Pts',(-19.3593953782732,-20.9816963774327,
8.54920519792616));
#163292=CARTESIAN_POINT('Ctrl Pts',(-19.1938962328857,-21.0254702954223,
8.53769565257752));
#163293=CARTESIAN_POINT('Ctrl Pts',(-18.9884995560309,-21.0539687658188,
8.52446063874565));
#163294=CARTESIAN_POINT('Ctrl Pts',(-18.9519275397863,-21.0580747093034,
8.52214624293066));
#163295=CARTESIAN_POINT('Ctrl Pts',(-18.9081487281184,-21.0618370152749,
8.51944039196791));
#163296=CARTESIAN_POINT('Ctrl Pts',(-18.9010296260911,-21.0624125468391,
8.51900241550412));
#163297=CARTESIAN_POINT('Ctrl Pts',(-18.8894081142736,-21.0632928929596,
8.51829091618393));
#163298=CARTESIAN_POINT('Ctrl Pts',(-18.8849074690118,-21.0636193545504,
8.51801622369394));
#163299=CARTESIAN_POINT('Ctrl Pts',(-18.8768483357869,-21.0641780391561,
8.51752590339475));
#163300=CARTESIAN_POINT('Ctrl Pts',(-18.873290286326,-21.0644156629017,
8.51730997738185));
#163301=CARTESIAN_POINT('Ctrl Pts',(-18.8655823236398,-21.0649108782469,
8.51684339699508));
#163302=CARTESIAN_POINT('Ctrl Pts',(-18.8614322600133,-21.0651652342161,
8.51659292568282));
#163303=CARTESIAN_POINT('Ctrl Pts',(-18.8498347035972,-21.0658417547009,
8.51589497574586));
#163304=CARTESIAN_POINT('Ctrl Pts',(-18.8423856045028,-21.0662367906572,
8.51544899174819));
#163305=CARTESIAN_POINT('Ctrl Pts',(-18.7990588277555,-21.0683048791342,
8.51286759802681));
#163306=CARTESIAN_POINT('Ctrl Pts',(-18.7631430029587,-21.069104159827,
8.51077801754748));
#163307=CARTESIAN_POINT('Ctrl Pts',(-18.6474957955114,-21.0687338852646,
8.5041620960288));
#163308=CARTESIAN_POINT('Ctrl Pts',(-18.5678412158585,-21.0639750380824,
8.49977578619877));
#163309=CARTESIAN_POINT('Ctrl Pts',(-18.3036801491088,-21.0331510336362,
8.48527562108297));
#163310=CARTESIAN_POINT('Ctrl Pts',(-18.1223981311488,-20.9872646006947,
8.47531905426197));
#163311=CARTESIAN_POINT('Ctrl Pts',(-17.9289803466747,-20.910090509261,
8.46320670677209));
#163312=CARTESIAN_POINT('Ctrl Pts',(-17.9086323605582,-20.9016008028846,
8.46191422976705));
#163313=CARTESIAN_POINT('Ctrl Pts',(-17.8806749270881,-20.8894201184571,
8.46011153633482));
#163314=CARTESIAN_POINT('Ctrl Pts',(-17.8729489924917,-20.8859988507716,
8.45961049806933));
#163315=CARTESIAN_POINT('Ctrl Pts',(-17.8597034183816,-20.880038225699,
8.4587464682755));
#163316=CARTESIAN_POINT('Ctrl Pts',(-17.854173809767,-20.8775211726134,
8.4583842448822));
#163317=CARTESIAN_POINT('Ctrl Pts',(-17.8427959033876,-20.872282756824,
8.45763575052938));
#163318=CARTESIAN_POINT('Ctrl Pts',(-17.836949060963,-20.8695584004975,
8.45724937916552));
#163319=CARTESIAN_POINT('Ctrl Pts',(-17.8233708417995,-20.863155890743,
8.45634800722608));
#163320=CARTESIAN_POINT('Ctrl Pts',(-17.815649186299,-20.8594574915572,
8.45583230835775));
#163321=CARTESIAN_POINT('Ctrl Pts',(-17.7910016155376,-20.8474678252563,
8.45417609692816));
#163322=CARTESIAN_POINT('Ctrl Pts',(-17.7741642716613,-20.8389975008534,
8.45302935925771));
#163323=CARTESIAN_POINT('Ctrl Pts',(-17.6906005878337,-20.7955515305975,
8.44725942685276));
#163324=CARTESIAN_POINT('Ctrl Pts',(-17.625668455206,-20.7572599801814,
8.44251982661224));
#163325=CARTESIAN_POINT('Ctrl Pts',(-17.4719767714351,-20.6552040417191,
8.43066394306269));
#163326=CARTESIAN_POINT('Ctrl Pts',(-17.3858467206001,-20.5878746591772,
8.42344782931245));
#163327=CARTESIAN_POINT('Ctrl Pts',(-17.2943200560022,-20.5041701034149,
8.4152543163928));
#163328=CARTESIAN_POINT('Ctrl Pts',(-17.2834467535492,-20.4940135063644,
8.41427197343938));
#163329=CARTESIAN_POINT('Ctrl Pts',(-17.1974992093132,-20.4120175456383,
8.40643936815063));
#163330=CARTESIAN_POINT('Ctrl Pts',(-17.1276903443813,-20.3348450158144,
8.39965269953485));
#163331=CARTESIAN_POINT('Ctrl Pts',(-17.0578732896386,-20.2452061300157,
8.39263281344571));
#163332=CARTESIAN_POINT('Ctrl Pts',(-17.051973056526,-20.2375225449252,
8.39203759938184));
#163333=CARTESIAN_POINT('Ctrl Pts',(-17.0433382645071,-20.2261166438656,
8.39116393487499));
#163334=CARTESIAN_POINT('Ctrl Pts',(-17.040562906277,-20.2224255730153,
8.39088272342314));
#163335=CARTESIAN_POINT('Ctrl Pts',(-17.0356601843566,-20.215860615268,
8.39038528633653));
#163336=CARTESIAN_POINT('Ctrl Pts',(-17.0335280033612,-20.2129903939172,
8.39016872630794));
#163337=CARTESIAN_POINT('Ctrl Pts',(-17.0289748072546,-20.2068285887528,
8.38970579404272));
#163338=CARTESIAN_POINT('Ctrl Pts',(-17.0265560534325,-20.2035354030259,
8.38945957833202));
#163339=CARTESIAN_POINT('Ctrl Pts',(-17.0199416512347,-20.1944748857733,
8.38878538982269));
#163340=CARTESIAN_POINT('Ctrl Pts',(-17.0157655443105,-20.1886932616161,
8.38835875092838));
#163341=CARTESIAN_POINT('Ctrl Pts',(-16.9936087030843,-20.1576892623538,
8.38608925195583));
#163342=CARTESIAN_POINT('Ctrl Pts',(-16.9761529312783,-20.1320942228667,
8.38428024199847));
#163343=CARTESIAN_POINT('Ctrl Pts',(-16.8701166337873,-19.9690385675996,
8.3730931893538));
#163344=CARTESIAN_POINT('Ctrl Pts',(-16.7971426030127,-19.8220715030235,
8.36445040393977));
#163345=CARTESIAN_POINT('Ctrl Pts',(-16.7019828385438,-19.5573573844441,
8.34905532959519));
#163346=CARTESIAN_POINT('Ctrl Pts',(-16.6714707864458,-19.443446031986,
8.34248547274969));
#163347=CARTESIAN_POINT('Ctrl Pts',(-16.6480483539502,-19.3135235243138,
8.33475159435991));
#163348=CARTESIAN_POINT('Ctrl Pts',(-16.6456537438723,-19.2994239886114,
8.33390942208875));
#163349=CARTESIAN_POINT('Ctrl Pts',(-16.6420705810909,-19.2769489874491,
8.33256197780976));
#163350=CARTESIAN_POINT('Ctrl Pts',(-16.6407890290309,-19.2685886384396,
8.33205965298254));
#163351=CARTESIAN_POINT('Ctrl Pts',(-16.6386174752184,-19.2538323582939,
8.33117101431345));
#163352=CARTESIAN_POINT('Ctrl Pts',(-16.6377065683066,-19.2474395784026,
8.33078536758771));
#163353=CARTESIAN_POINT('Ctrl Pts',(-16.6358832777938,-19.2342105354972,
8.32998590175462));
#163354=CARTESIAN_POINT('Ctrl Pts',(-16.6349750261165,-19.2273737888929,
8.32957195685239));
#163355=CARTESIAN_POINT('Ctrl Pts',(-16.6327299132914,-19.2098172290993,
8.32850689665191));
#163356=CARTESIAN_POINT('Ctrl Pts',(-16.6314416807036,-19.1990914974247,
8.32785425434452));
#163357=CARTESIAN_POINT('Ctrl Pts',(-16.6264111796692,-19.1543159671652,
8.32512123162497));
#163358=CARTESIAN_POINT('Ctrl Pts',(-16.6234136981773,-19.1201892783728,
8.32301758462311));
#163359=CARTESIAN_POINT('Ctrl Pts',(-16.6177644663944,-19.0311230801942,
8.31747054484192));
#163360=CARTESIAN_POINT('Ctrl Pts',(-16.616423491967,-18.9761290671421,
8.31398889466164));
#163361=CARTESIAN_POINT('Ctrl Pts',(-16.6188176927005,-18.8118575412607,
8.30342980202159));
#163362=CARTESIAN_POINT('Ctrl Pts',(-16.6288723228099,-18.7028612911686,
8.29620393433791));
#163363=CARTESIAN_POINT('Ctrl Pts',(-16.6537707620644,-18.5572707146935,
8.28644680181537));
#163364=CARTESIAN_POINT('Ctrl Pts',(-16.6612764451272,-18.5195857806304,
8.28391287315826));
#163365=CARTESIAN_POINT('Ctrl Pts',(-16.6768654437478,-18.4511020719063,
8.27931156440573));
#163366=CARTESIAN_POINT('Ctrl Pts',(-16.6846260405109,-18.4202408199611,
8.27723942090632));
#163367=CARTESIAN_POINT('Ctrl Pts',(-16.7062965662911,-18.3416044616206,
8.27198047353112));
#163368=CARTESIAN_POINT('Ctrl Pts',(-16.7212012470447,-18.2941200952936,
8.2688248791707));
#163369=CARTESIAN_POINT('Ctrl Pts',(-16.7403666535599,-18.2398370469197,
8.26527477879738));
#163370=CARTESIAN_POINT('Ctrl Pts',(-16.7430074693989,-18.23248715149,8.26479533853439));
#163371=CARTESIAN_POINT('Ctrl Pts',(-16.7472898090156,-18.2207727048025,
8.26403337285371));
#163372=CARTESIAN_POINT('Ctrl Pts',(-16.7489051545586,-18.2163987522008,
8.26374935641675));
#163373=CARTESIAN_POINT('Ctrl Pts',(-16.7517898959555,-18.2086662972588,
8.26324816923809));
#163374=CARTESIAN_POINT('Ctrl Pts',(-16.7530534007978,-18.2053056434818,
8.2630306512886));
#163375=CARTESIAN_POINT('Ctrl Pts',(-16.7557475569954,-18.1981947319117,
8.26257106179847));
#163376=CARTESIAN_POINT('Ctrl Pts',(-16.757180323144,-18.1944453311721,
8.26232911903495));
#163377=CARTESIAN_POINT('Ctrl Pts',(-16.7610713735858,-18.1843490635763,
8.26167860951522));
#163378=CARTESIAN_POINT('Ctrl Pts',(-16.763549640883,-18.1780098771641,
8.26127122451134));
#163379=CARTESIAN_POINT('Ctrl Pts',(-16.7759382354572,-18.1467661404363,
8.25926805224283));
#163380=CARTESIAN_POINT('Ctrl Pts',(-16.7862908387133,-18.1220381834663,
8.25769739569592));
#163381=CARTESIAN_POINT('Ctrl Pts',(-16.8174918675877,-18.0513140161821,
8.25322967169033));
#163382=CARTESIAN_POINT('Ctrl Pts',(-16.8395206619337,-18.0058565745763,
8.25038829739416));
#163383=CARTESIAN_POINT('Ctrl Pts',(-16.9254735306056,-17.8435544509589,
8.24020469132456));
#163384=CARTESIAN_POINT('Ctrl Pts',(-16.9987556897927,-17.7320208339459,
8.233113323117));
#163385=CARTESIAN_POINT('Ctrl Pts',(-17.1463019961067,-17.5479109261272,
8.22012759393819));
#163386=CARTESIAN_POINT('Ctrl Pts',(-17.2163181498419,-17.4725105796423,
8.21435056080368));
#163387=CARTESIAN_POINT('Ctrl Pts',(-17.301797446402,-17.3929356121952,
8.20750654813196));
#163388=CARTESIAN_POINT('Ctrl Pts',(-17.3121631560534,-17.3834765239503,
8.20667997387138));
#163389=CARTESIAN_POINT('Ctrl Pts',(-17.3288678445816,-17.3685345443103,
8.20535283851313));
#163390=CARTESIAN_POINT('Ctrl Pts',(-17.335146779248,-17.3629849317064,
8.20485508566195));
#163391=CARTESIAN_POINT('Ctrl Pts',(-17.3463126612305,-17.3532334800671,
8.2039717585113));
#163392=CARTESIAN_POINT('Ctrl Pts',(-17.3511861840082,-17.3490163805192,
8.20358682574884));
#163393=CARTESIAN_POINT('Ctrl Pts',(-17.3613395453493,-17.3403113533169,
8.20278608565162));
#163394=CARTESIAN_POINT('Ctrl Pts',(-17.3666223085158,-17.335826969454,
8.20237013890804));
#163395=CARTESIAN_POINT('Ctrl Pts',(-17.380310476479,-17.3243226352403,
8.2012940592386));
#163396=CARTESIAN_POINT('Ctrl Pts',(-17.3887484289872,-17.3173418909536,
8.20063233785863));
#163397=CARTESIAN_POINT('Ctrl Pts',(-17.4248203013454,-17.2879679700368,
8.19781002618102));
#163398=CARTESIAN_POINT('Ctrl Pts',(-17.4529607662872,-17.2662086959234,
8.19562422574354));
#163399=CARTESIAN_POINT('Ctrl Pts',(-17.5283393636975,-17.2109006007498,
8.18980676424299));
#163400=CARTESIAN_POINT('Ctrl Pts',(-17.5764272690172,-17.1785657281854,
8.18613203196921));
#163401=CARTESIAN_POINT('Ctrl Pts',(-17.7321239993493,-17.0829060098374,
8.17436007484872));
#163402=CARTESIAN_POINT('Ctrl Pts',(-17.8440352885071,-17.0271035539912,
8.16606298531998));
#163403=CARTESIAN_POINT('Ctrl Pts',(-18.0517389461217,-16.9455402139504,
8.15136548787617));
#163404=CARTESIAN_POINT('Ctrl Pts',(-18.1456854416631,-16.9160109065311,
8.14495948673951));
#163405=CARTESIAN_POINT('Ctrl Pts',(-18.2507828585176,-16.8908633776633,
8.13828278962362));
#163406=CARTESIAN_POINT('Ctrl Pts',(-18.2602267227462,-16.8886721366385,
8.13768713311243));
#163407=CARTESIAN_POINT('Ctrl Pts',(-18.2741924276083,-16.8855326435766,
8.13681294558019));
#163408=CARTESIAN_POINT('Ctrl Pts',(-18.2787026988469,-16.8845342306851,
8.13653164887833));
#163409=CARTESIAN_POINT('Ctrl Pts',(-18.2867098962466,-16.8827891967365,
8.13603411755249));
#163410=CARTESIAN_POINT('Ctrl Pts',(-18.2902054786241,-16.8820366648816,
8.13581754806249));
#163411=CARTESIAN_POINT('Ctrl Pts',(-18.2976987885946,-16.8804433532068,
8.13535465812819));
#163412=CARTESIAN_POINT('Ctrl Pts',(-18.3016970369502,-16.8796052893491,
8.13510849388291));
#163413=CARTESIAN_POINT('Ctrl Pts',(-18.3126783341471,-16.8773366869619,
8.13443459149671));
#163414=CARTESIAN_POINT('Ctrl Pts',(-18.3196662953568,-16.8759298198108,
8.13400818537423));
#163415=CARTESIAN_POINT('Ctrl Pts',(-18.3570042660396,-16.8686087005114,
8.13174214672186));
#163416=CARTESIAN_POINT('Ctrl Pts',(-18.387475715922,-16.8633242861216,
8.12993624215545));
#163417=CARTESIAN_POINT('Ctrl Pts',(-18.4800427207798,-16.8493528899776,
8.12455147563203));
#163418=CARTESIAN_POINT('Ctrl Pts',(-18.5424214181053,-16.8427541716602,
8.12105933631858));
#163419=CARTESIAN_POINT('Ctrl Pts',(-18.7637451850993,-16.8292431758982,
8.10887303959188));
#163420=CARTESIAN_POINT('Ctrl Pts',(-18.9230660517177,-16.8374703224713,
8.10043034806301));
#163421=CARTESIAN_POINT('Ctrl Pts',(-19.1420313286223,-16.8737417427372,
8.08794424482075));
#163422=CARTESIAN_POINT('Ctrl Pts',(-19.2036036178517,-16.8867837176131,
8.08433871609616));
#163423=CARTESIAN_POINT('Ctrl Pts',(-19.2765795790497,-16.9056735129481,
8.07991173654676));
#163424=CARTESIAN_POINT('Ctrl Pts',(-19.2886310067931,-16.9089069704164,
8.07917560545274));
#163425=CARTESIAN_POINT('Ctrl Pts',(-19.3083636106948,-16.9143887796491,
8.07796169024569));
#163426=CARTESIAN_POINT('Ctrl Pts',(-19.3160619743844,-16.9165745167466,
8.0774859405849));
#163427=CARTESIAN_POINT('Ctrl Pts',(-19.3298740587001,-16.920580841761,
8.07662840870397));
#163428=CARTESIAN_POINT('Ctrl Pts',(-19.3359923217147,-16.9223855209641,
8.07624714963469));
#163429=CARTESIAN_POINT('Ctrl Pts',(-19.3489988214337,-16.926285980401,
8.07543362036338));
#163430=CARTESIAN_POINT('Ctrl Pts',(-19.3558846960423,-16.9283893006809,
8.07500110721256));
#163431=CARTESIAN_POINT('Ctrl Pts',(-19.3743834357377,-16.9341431568496,
8.07383421152724));
#163432=CARTESIAN_POINT('Ctrl Pts',(-19.3859756338509,-16.9378587568447,
8.07309770024815));
#163433=CARTESIAN_POINT('Ctrl Pts',(-19.4428680027367,-16.9566368439457,
8.06945651097606));
#163434=CARTESIAN_POINT('Ctrl Pts',(-19.487678795483,-16.9731276782839,
8.06650496813699));
#163435=CARTESIAN_POINT('Ctrl Pts',(-19.6873900263417,-17.0543910295399,
8.05295881836857));
#163436=CARTESIAN_POINT('Ctrl Pts',(-19.8347920683046,-17.1359293467963,
8.04180809482539));
#163437=CARTESIAN_POINT('Ctrl Pts',(-20.0511529844362,-17.2917125524852,
8.02424610210403));
#163438=CARTESIAN_POINT('Ctrl Pts',(-20.1271874451664,-17.3549778438416,
8.01781051800602));
#163439=CARTESIAN_POINT('Ctrl Pts',(-20.2055328067276,-17.4300360762429,
8.01110703749204));
#163440=CARTESIAN_POINT('Ctrl Pts',(-20.2124872558412,-17.4367909619418,
8.0105113657937));
#163441=CARTESIAN_POINT('Ctrl Pts',(-20.222686653473,-17.4468347642197,
8.00963716030919));
#163442=CARTESIAN_POINT('Ctrl Pts',(-20.2259675191544,-17.4500867994614,
8.00935586068171));
#163443=CARTESIAN_POINT('Ctrl Pts',(-20.2317689984,-17.4558750678084,8.00885832612126));
#163444=CARTESIAN_POINT('Ctrl Pts',(-20.2342938548486,-17.4584069714019,
8.00864175630607));
#163445=CARTESIAN_POINT('Ctrl Pts',(-20.2396895475206,-17.4638452116159,
8.00817886782222));
#163446=CARTESIAN_POINT('Ctrl Pts',(-20.2425583820697,-17.4667534560756,
8.00793270534137));
#163447=CARTESIAN_POINT('Ctrl Pts',(-20.2484282710288,-17.4727385340698,
8.00742888691748));
#163448=CARTESIAN_POINT('Ctrl Pts',(-20.2514284117591,-17.4758162415899,
8.00717130164949));
#163449=CARTESIAN_POINT('Ctrl Pts',(-20.2651717970894,-17.4900011242649,
8.00599083471941));
#163450=CARTESIAN_POINT('Ctrl Pts',(-20.2758029232494,-17.5012169142555,
8.00507630456515));
#163451=CARTESIAN_POINT('Ctrl Pts',(-20.3409160821033,-17.571435220624,
7.99945873370742));
#163452=CARTESIAN_POINT('Ctrl Pts',(-20.39213258708,-17.6333880502048,7.99496712675279));
#163453=CARTESIAN_POINT('Ctrl Pts',(-20.4809155745372,-17.7541623327641,
7.98672646257819));
#163454=CARTESIAN_POINT('Ctrl Pts',(-20.519334737261,-17.8122152080738,
7.98296345890495));
#163455=CARTESIAN_POINT('Ctrl Pts',(-20.6215836030318,-17.984610550139,
7.97207000000856));
#163456=CARTESIAN_POINT('Ctrl Pts',(-20.6777317100981,-18.1030631176663,
7.96490146909176));
#163457=CARTESIAN_POINT('Ctrl Pts',(-20.7225806049454,-18.2258896932043,
7.9573447159704));
#163458=CARTESIAN_POINT('Ctrl Pts',(-20.722580563188,-18.2258895788442,
7.73405224475127));
#163459=CARTESIAN_POINT('Ctrl Pts',(-20.7064128399083,-18.1816114369415,
7.73716571128361));
#163460=CARTESIAN_POINT('Ctrl Pts',(-20.6887553875351,-18.1378434671757,
7.74027545263082));
#163461=CARTESIAN_POINT('Ctrl Pts',(-20.6434178114597,-18.0354839604616,
7.74757888317297));
#163462=CARTESIAN_POINT('Ctrl Pts',(-20.6145038161139,-17.9775334631239,
7.75173863385529));
#163463=CARTESIAN_POINT('Ctrl Pts',(-20.5765961428692,-17.9095509041066,
7.75657433186193));
#163464=CARTESIAN_POINT('Ctrl Pts',(-20.5701090062428,-17.8981668062722,
7.75738252215286));
#163465=CARTESIAN_POINT('Ctrl Pts',(-20.5608902039258,-17.8823325624502,
7.75850363688409));
#163466=CARTESIAN_POINT('Ctrl Pts',(-20.5582472891404,-17.8778314501188,
7.75882198702271));
#163467=CARTESIAN_POINT('Ctrl Pts',(-20.5537180050429,-17.8701826181471,
7.75936231920705));
#163468=CARTESIAN_POINT('Ctrl Pts',(-20.5518400585604,-17.8670299599633,
7.7595848423397));
#163469=CARTESIAN_POINT('Ctrl Pts',(-20.5482251303688,-17.8609970261551,
7.76001027891682));
#163470=CARTESIAN_POINT('Ctrl Pts',(-20.5464894768557,-17.8581159982644,
7.76021327947346));
#163471=CARTESIAN_POINT('Ctrl Pts',(-20.5418745762555,-17.8504968196842,
7.76074972697087));
#163472=CARTESIAN_POINT('Ctrl Pts',(-20.5389835463727,-17.845765784917,
7.76108240755892));
#163473=CARTESIAN_POINT('Ctrl Pts',(-20.5286654492863,-17.8290288404219,
7.76225803761003));
#163474=CARTESIAN_POINT('Ctrl Pts',(-20.5211367272519,-17.8170856234111,
7.76309458195114));
#163475=CARTESIAN_POINT('Ctrl Pts',(-20.4134239879594,-17.6499451696352,
7.7747813095825));
#163476=CARTESIAN_POINT('Ctrl Pts',(-20.2934511417893,-17.5084120593278,
7.7844807955985));
#163477=CARTESIAN_POINT('Ctrl Pts',(-20.0777212262056,-17.3126557582604,
7.80042941649284));
#163478=CARTESIAN_POINT('Ctrl Pts',(-19.9935533610791,-17.2471370468884,
7.80636528465145));
#163479=CARTESIAN_POINT('Ctrl Pts',(-19.891973940479,-17.1797068355112,
7.81345558541181));
#163480=CARTESIAN_POINT('Ctrl Pts',(-19.8790362014658,-17.1713206951283,
7.81435714305201));
#163481=CARTESIAN_POINT('Ctrl Pts',(-19.8582148828919,-17.1581452249403,
7.81580629229157));
#163482=CARTESIAN_POINT('Ctrl Pts',(-19.8503894576543,-17.1532647132715,
7.81635054159525));
#163483=CARTESIAN_POINT('Ctrl Pts',(-19.8354248252234,-17.1440669376494,
7.81739070243876));
#163484=CARTESIAN_POINT('Ctrl Pts',(-19.8282914839594,-17.1397404301115,
7.81788626429294));
#163485=CARTESIAN_POINT('Ctrl Pts',(-19.8157043192226,-17.1322074873853,
7.81876033434981));
#163486=CARTESIAN_POINT('Ctrl Pts',(-19.8102613169945,-17.128983105017,
7.81913818143699));
#163487=CARTESIAN_POINT('Ctrl Pts',(-19.7995714103964,-17.122715067949,
7.81988005997206));
#163488=CARTESIAN_POINT('Ctrl Pts',(-19.7943257125952,-17.1196694688725,
7.82024401600125));
#163489=CARTESIAN_POINT('Ctrl Pts',(-19.7817739058485,-17.112453966543,
7.82111469269163));
#163490=CARTESIAN_POINT('Ctrl Pts',(-19.7744559305445,-17.1083050088522,
7.82162216321626));
#163491=CARTESIAN_POINT('Ctrl Pts',(-19.7480707207454,-17.0935529177603,
7.82345144352715));
#163492=CARTESIAN_POINT('Ctrl Pts',(-19.7288650789912,-17.0832013476949,
7.82478219698052));
#163493=CARTESIAN_POINT('Ctrl Pts',(-19.5423649987559,-16.9863701229919,
7.83770155073751));
#163494=CARTESIAN_POINT('Ctrl Pts',(-19.3644237530526,-16.9222975968582,
7.85011675049619));
#163495=CARTESIAN_POINT('Ctrl Pts',(-19.1037882958569,-16.8660734356316,
7.86771526563253));
#163496=CARTESIAN_POINT('Ctrl Pts',(-19.0263027631822,-16.8538117887825,
7.87286101300327));
#163497=CARTESIAN_POINT('Ctrl Pts',(-18.9129431818249,-16.8422767521664,
7.88012149218994));
#163498=CARTESIAN_POINT('Ctrl Pts',(-18.8774876893382,-16.8395690608061,
7.88235431312799));
#163499=CARTESIAN_POINT('Ctrl Pts',(-18.834551196034,-16.8373762117033,
7.88499914338855));
#163500=CARTESIAN_POINT('Ctrl Pts',(-18.8271217958068,-16.8370360182797,
7.88545464626501));
#163501=CARTESIAN_POINT('Ctrl Pts',(-18.815541117558,-16.8365668781853,
7.88616117413427));
#163502=CARTESIAN_POINT('Ctrl Pts',(-18.8113910766774,-16.8364109877724,
7.88641366597596));
#163503=CARTESIAN_POINT('Ctrl Pts',(-18.8036761892909,-16.8361439206245,
7.88688171322755));
#163504=CARTESIAN_POINT('Ctrl Pts',(-18.8001115551385,-16.8360295411958,
7.88709744007462));
#163505=CARTESIAN_POINT('Ctrl Pts',(-18.7920294467235,-16.8357906517782,
7.88758536496168));
#163506=CARTESIAN_POINT('Ctrl Pts',(-18.7875118639231,-16.835671598386,
7.88785725477571));
#163507=CARTESIAN_POINT('Ctrl Pts',(-18.7741086738836,-16.8353613242715,
7.88866151892859));
#163508=CARTESIAN_POINT('Ctrl Pts',(-18.7652220780536,-16.8352115888903,
7.88919162886611));
#163509=CARTESIAN_POINT('Ctrl Pts',(-18.6985800938075,-16.8345084680831,
7.89314525863192));
#163510=CARTESIAN_POINT('Ctrl Pts',(-18.6408191802611,-16.8362628812182,
7.89644973370444));
#163511=CARTESIAN_POINT('Ctrl Pts',(-18.522535678257,-16.8447101683218,
7.90309500099272));
#163512=CARTESIAN_POINT('Ctrl Pts',(-18.4620860861765,-16.8516545308491,
7.90642560168815));
#163513=CARTESIAN_POINT('Ctrl Pts',(-18.2937982284971,-16.8783756448379,
7.9157039176958));
#163514=CARTESIAN_POINT('Ctrl Pts',(-18.1870778452132,-16.9039348484223,
7.92160300739493));
#163515=CARTESIAN_POINT('Ctrl Pts',(-18.0301233226179,-16.9546733587603,
7.93077292256164));
#163516=CARTESIAN_POINT('Ctrl Pts',(-17.978119045525,-16.9737686136473,
7.93389510610662));
#163517=CARTESIAN_POINT('Ctrl Pts',(-17.8950957247024,-17.008005644186,
7.939061225924));
#163518=CARTESIAN_POINT('Ctrl Pts',(-17.8635921539698,-17.0219055925997,
7.94106532902854));
#163519=CARTESIAN_POINT('Ctrl Pts',(-17.82265030938,-17.0411761258368,7.94373396937426));
#163520=CARTESIAN_POINT('Ctrl Pts',(-17.8128934636106,-17.0458602153299,
7.94437479746725));
#163521=CARTESIAN_POINT('Ctrl Pts',(-17.7969747400603,-17.053653274655,
7.94542851168193));
#163522=CARTESIAN_POINT('Ctrl Pts',(-17.7907913133493,-17.0567179631818,
7.94583985072366));
#163523=CARTESIAN_POINT('Ctrl Pts',(-17.7788529906393,-17.062707840171,
7.94663802249728));
#163524=CARTESIAN_POINT('Ctrl Pts',(-17.7730962658295,-17.0656292286755,
7.94702471855074));
#163525=CARTESIAN_POINT('Ctrl Pts',(-17.7598378968045,-17.0724339460696,
7.94791956038673));
#163526=CARTESIAN_POINT('Ctrl Pts',(-17.7523459908732,-17.0763359155957,
7.94842835982288));
#163527=CARTESIAN_POINT('Ctrl Pts',(-17.7322665289405,-17.0869470489114,
7.94980061753591));
#163528=CARTESIAN_POINT('Ctrl Pts',(-17.7197232635144,-17.0937386772582,
7.95066699030041));
#163529=CARTESIAN_POINT('Ctrl Pts',(-17.60473489066,-17.1575109197283,7.95869539967728));
#163530=CARTESIAN_POINT('Ctrl Pts',(-17.5071362210139,-17.222772388048,
7.9661612959015));
#163531=CARTESIAN_POINT('Ctrl Pts',(-17.2873294541717,-17.3977630813291,
7.98451540409503));
#163532=CARTESIAN_POINT('Ctrl Pts',(-17.1714785741788,-17.5142812876717,
7.99554622791961));
#163533=CARTESIAN_POINT('Ctrl Pts',(-17.0508657251224,-17.66758285754,8.00792657309285));
#163534=CARTESIAN_POINT('Ctrl Pts',(-17.0320614474767,-17.6926057853608,
8.00988633973082));
#163535=CARTESIAN_POINT('Ctrl Pts',(-17.0096473637285,-17.7238517277554,
8.01225054448643));
#163536=CARTESIAN_POINT('Ctrl Pts',(-17.005506320073,-17.7296867035592,
8.01268857134638));
#163537=CARTESIAN_POINT('Ctrl Pts',(-16.999044113337,-17.738890850831,8.013373934371));
#163538=CARTESIAN_POINT('Ctrl Pts',(-16.9967030428386,-17.7422458845879,
8.01362260085474));
#163539=CARTESIAN_POINT('Ctrl Pts',(-16.9923346023716,-17.7485452142585,
8.01408729386359));
#163540=CARTESIAN_POINT('Ctrl Pts',(-16.9903049875185,-17.7514878250175,
8.01430346888001));
#163541=CARTESIAN_POINT('Ctrl Pts',(-16.9856749524421,-17.7582371339606,
8.01479726494388));
#163542=CARTESIAN_POINT('Ctrl Pts',(-16.9830795111358,-17.7620471879733,
8.01507454717582));
#163543=CARTESIAN_POINT('Ctrl Pts',(-16.9750918462323,-17.7738556304619,
8.01592948649624));
#163544=CARTESIAN_POINT('Ctrl Pts',(-16.9697417411951,-17.7818825473233,
8.01650437258235));
#163545=CARTESIAN_POINT('Ctrl Pts',(-16.9155649449674,-17.8643819225728,
8.0223521707813));
#163546=CARTESIAN_POINT('Ctrl Pts',(-16.8714223613125,-17.9418378282073,
8.02734001015806));
#163547=CARTESIAN_POINT('Ctrl Pts',(-16.7827976071741,-18.1230338385824,
8.03842756445445));
#163548=CARTESIAN_POINT('Ctrl Pts',(-16.7414626885364,-18.2280031130629,
8.04446085537161));
#163549=CARTESIAN_POINT('Ctrl Pts',(-16.6802635317126,-18.4291406182582,
8.05601404036221));
#163550=CARTESIAN_POINT('Ctrl Pts',(-16.6583468034821,-18.5243599834351,
8.06147987673573));
#163551=CARTESIAN_POINT('Ctrl Pts',(-16.639688862379,-18.642131126821,8.06842134191135));
#163552=CARTESIAN_POINT('Ctrl Pts',(-16.6366291201695,-18.6635676838346,
8.06969165974116));
#163553=CARTESIAN_POINT('Ctrl Pts',(-16.6327571281325,-18.6940283645074,
8.07150786018356));
#163554=CARTESIAN_POINT('Ctrl Pts',(-16.631673088893,-18.703017016143,8.07204516853453));
#163555=CARTESIAN_POINT('Ctrl Pts',(-16.6299059921746,-18.7185045919187,
8.07297341329497));
#163556=CARTESIAN_POINT('Ctrl Pts',(-16.6291952998433,-18.7250002817536,
8.07336347317768));
#163557=CARTESIAN_POINT('Ctrl Pts',(-16.6278943491678,-18.7374226009045,
8.07411087865853));
#163558=CARTESIAN_POINT('Ctrl Pts',(-16.6272990048547,-18.7433486434325,
8.07446805998439));
#163559=CARTESIAN_POINT('Ctrl Pts',(-16.6258203597634,-18.7587189147403,
8.07539615226743));
#163560=CARTESIAN_POINT('Ctrl Pts',(-16.6249755189458,-18.7681666320788,
8.07596826803302));
#163561=CARTESIAN_POINT('Ctrl Pts',(-16.6223307566067,-18.8001652658668,
8.07791169720951));
#163562=CARTESIAN_POINT('Ctrl Pts',(-16.6208288713611,-18.8227386416877,
8.07929231384713));
#163563=CARTESIAN_POINT('Ctrl Pts',(-16.6106129269325,-19.0252314023213,
8.09176743605281));
#163564=CARTESIAN_POINT('Ctrl Pts',(-16.6245364211876,-19.2055224334481,
8.10360854106691));
#163565=CARTESIAN_POINT('Ctrl Pts',(-16.6781115165114,-19.4638939837152,
8.12103774288842));
#163566=CARTESIAN_POINT('Ctrl Pts',(-16.6999871318218,-19.5448797417938,
8.12655346853805));
#163567=CARTESIAN_POINT('Ctrl Pts',(-16.7383595416392,-19.6594441144297,
8.13426182023935));
#163568=CARTESIAN_POINT('Ctrl Pts',(-16.7510294389671,-19.6942170530984,
8.13658795499996));
#163569=CARTESIAN_POINT('Ctrl Pts',(-16.7673655328663,-19.7356418091579,
8.13932784163553));
#163570=CARTESIAN_POINT('Ctrl Pts',(-16.7701631744504,-19.7426266747962,
8.1397887431273));
#163571=CARTESIAN_POINT('Ctrl Pts',(-16.7745698409565,-19.7534610761508,
8.14050179926466));
#163572=CARTESIAN_POINT('Ctrl Pts',(-16.7761530733518,-19.7573209405335,
8.14075546406796));
#163573=CARTESIAN_POINT('Ctrl Pts',(-16.7791102230181,-19.7644701018884,
8.14122457811287));
#163574=CARTESIAN_POINT('Ctrl Pts',(-16.7804810253747,-19.7677605792623,
8.14144020573326));
#163575=CARTESIAN_POINT('Ctrl Pts',(-16.78359865396,-19.7751912176479,8.14192650445766));
#163576=CARTESIAN_POINT('Ctrl Pts',(-16.7853503498512,-19.779329277421,
8.14219687597448));
#163577=CARTESIAN_POINT('Ctrl Pts',(-16.7905589121293,-19.791525232701,
8.14299250876281));
#163578=CARTESIAN_POINT('Ctrl Pts',(-16.7940527268698,-19.7995673789466,
8.14351557720641));
#163579=CARTESIAN_POINT('Ctrl Pts',(-16.8196579410273,-19.8575182172999,
8.14727492078615));
#163580=CARTESIAN_POINT('Ctrl Pts',(-16.8436444222827,-19.9065813928319,
8.15040498466973));
#163581=CARTESIAN_POINT('Ctrl Pts',(-16.9483938022009,-20.1013668974881,
8.16283012690631));
#163582=CARTESIAN_POINT('Ctrl Pts',(-17.0443251215857,-20.2382503401946,
8.17160212536566));
#163583=CARTESIAN_POINT('Ctrl Pts',(-17.1953721150083,-20.407310071935,
8.18415921306798));
#163584=CARTESIAN_POINT('Ctrl Pts',(-17.237315371547,-20.4504116571376,
8.18753676215937));
#163585=CARTESIAN_POINT('Ctrl Pts',(-17.3076002275277,-20.5167386396994,
8.19308610234129));
#163586=CARTESIAN_POINT('Ctrl Pts',(-17.3348100063349,-20.5411162472607,
8.19520985096362));
#163587=CARTESIAN_POINT('Ctrl Pts',(-17.3710587847143,-20.5719390393808,
8.19801499843072));
#163588=CARTESIAN_POINT('Ctrl Pts',(-17.3795377741847,-20.5790351315997,
8.19866948196454));
#163589=CARTESIAN_POINT('Ctrl Pts',(-17.3934384697376,-20.5904847034837,
8.19973994790185));
#163590=CARTESIAN_POINT('Ctrl Pts',(-17.398826791147,-20.5948785227637,
8.20015428573892));
#163591=CARTESIAN_POINT('Ctrl Pts',(-17.4092449560198,-20.6032887401418,
8.20095428269114));
#163592=CARTESIAN_POINT('Ctrl Pts',(-17.4142716712209,-20.6073089037002,
8.20133978386204));
#163593=CARTESIAN_POINT('Ctrl Pts',(-17.4258434876823,-20.6164773600247,
8.20222614651633));
#163594=CARTESIAN_POINT('Ctrl Pts',(-17.4324007570282,-20.6216100593716,
8.20272762251858));
#163595=CARTESIAN_POINT('Ctrl Pts',(-17.4499464357885,-20.635177749541,
8.20406745434208));
#163596=CARTESIAN_POINT('Ctrl Pts',(-17.4609875035442,-20.6435436919763,
8.20490851402931));
#163597=CARTESIAN_POINT('Ctrl Pts',(-17.5485731123447,-20.7085651051935,
8.2115652898949));
#163598=CARTESIAN_POINT('Ctrl Pts',(-17.6287689212071,-20.7600978384549,
8.21757796912536));
#163599=CARTESIAN_POINT('Ctrl Pts',(-17.8666860067105,-20.8912241964742,
8.23516021750516));
#163600=CARTESIAN_POINT('Ctrl Pts',(-18.0312480610021,-20.956733889124,
8.24707830459643));
#163601=CARTESIAN_POINT('Ctrl Pts',(-18.2411031019634,-21.0112163482422,
8.26095040543944));
#163602=CARTESIAN_POINT('Ctrl Pts',(-18.2804700466945,-21.020243311074,
8.2634945107724));
#163603=CARTESIAN_POINT('Ctrl Pts',(-18.3276368306253,-21.029647093671,
8.26645492923893));
#163604=CARTESIAN_POINT('Ctrl Pts',(-18.3352080622418,-21.0311136250433,
8.26692746196168));
#163605=CARTESIAN_POINT('Ctrl Pts',(-18.3469272755842,-21.033317239552,
8.2676545660457));
#163606=CARTESIAN_POINT('Ctrl Pts',(-18.3510696362545,-21.0340833515683,
8.2679107426953));
#163607=CARTESIAN_POINT('Ctrl Pts',(-18.3587183347677,-21.0354743473582,
8.26838219448369));
#163608=CARTESIAN_POINT('Ctrl Pts',(-18.3622239363282,-21.0361027429494,
8.2685976627388));
#163609=CARTESIAN_POINT('Ctrl Pts',(-18.3701052891988,-21.0374949938178,
8.26908072072117));
#163610=CARTESIAN_POINT('Ctrl Pts',(-18.3744818546361,-21.038253923608,
8.26934802835015));
#163611=CARTESIAN_POINT('Ctrl Pts',(-18.3856745709076,-21.0401585588766,
8.27002932558514));
#163612=CARTESIAN_POINT('Ctrl Pts',(-18.392494063199,-21.0412846789427,
8.27044222896896));
#163613=CARTESIAN_POINT('Ctrl Pts',(-18.4321427621243,-21.0476326542295,
8.27283074398952));
#163614=CARTESIAN_POINT('Ctrl Pts',(-18.4650877743743,-21.0521144028249,
8.27476723001864));
#163615=CARTESIAN_POINT('Ctrl Pts',(-18.5166187648994,-21.057891890517,
8.27774022926928));
#163616=CARTESIAN_POINT('Ctrl Pts',(-18.5351378889324,-21.0597213178523,
8.27879745117047));
#163617=CARTESIAN_POINT('Ctrl Pts',(-18.584826517633,-21.0639691089502,
8.2816096837538));
#163618=CARTESIAN_POINT('Ctrl Pts',(-18.6160300361049,-21.0659416881649,
8.2833500780702));
#163619=CARTESIAN_POINT('Ctrl Pts',(-18.685727195702,-21.0687995721619,
8.28720181338053));
#163620=CARTESIAN_POINT('Ctrl Pts',(-18.724224353658,-21.0693273855509,
8.28930516530339));
#163621=CARTESIAN_POINT('Ctrl Pts',(-18.8719903821001,-21.0673228852339,
8.29735059947384));
#163622=CARTESIAN_POINT('Ctrl Pts',(-18.9809855977799,-21.0573810765956,
8.30323552927093));
#163623=CARTESIAN_POINT('Ctrl Pts',(-19.1429758788192,-21.0298489536488,
8.3123725185757));
#163624=CARTESIAN_POINT('Ctrl Pts',(-19.1968465462121,-21.0185163863954,
8.31547582423037));
#163625=CARTESIAN_POINT('Ctrl Pts',(-19.2834498509849,-20.9967416608092,
8.32061348617363));
#163626=CARTESIAN_POINT('Ctrl Pts',(-19.3164784119609,-20.9875791072288,
8.32260858218581));
#163627=CARTESIAN_POINT('Ctrl Pts',(-19.3596071828885,-20.9744790228416,
8.32526692416244));
#163628=CARTESIAN_POINT('Ctrl Pts',(-19.3699213128256,-20.9712597213976,
8.32590669380477));
#163629=CARTESIAN_POINT('Ctrl Pts',(-19.3867783020085,-20.9658562662151,
8.32695911045069));
#163630=CARTESIAN_POINT('Ctrl Pts',(-19.3933360107177,-20.963718816283,
8.32737021783749));
#163631=CARTESIAN_POINT('Ctrl Pts',(-19.4060125478574,-20.9595183264037,
8.32816825662581));
#163632=CARTESIAN_POINT('Ctrl Pts',(-19.4121326197196,-20.9574592601107,
8.32855505302561));
#163633=CARTESIAN_POINT('Ctrl Pts',(-19.4262461219506,-20.9526388544784,
8.32945058814828));
#163634=CARTESIAN_POINT('Ctrl Pts',(-19.4342325773197,-20.9498575659497,
8.32995998372255));
#163635=CARTESIAN_POINT('Ctrl Pts',(-19.455675830892,-20.9422455663165,
8.33133489276266));
#163636=CARTESIAN_POINT('Ctrl Pts',(-19.4691005302265,-20.9373263242738,
8.33220333827866));
#163637=CARTESIAN_POINT('Ctrl Pts',(-19.5923289341096,-20.8907502524256,
8.34024725615454));
#163638=CARTESIAN_POINT('Ctrl Pts',(-19.6985200913806,-20.8401668818351,
8.34772772085121));
#163639=CARTESIAN_POINT('Ctrl Pts',(-19.9414515005513,-20.6985882753817,
8.36609796588657));
#163640=CARTESIAN_POINT('Ctrl Pts',(-20.0728963838703,-20.599988625582,
8.3771289983232));
#163641=CARTESIAN_POINT('Ctrl Pts',(-20.2141769019647,-20.465845864836,
8.38949103861084));
#163642=CARTESIAN_POINT('Ctrl Pts',(-20.2362207773434,-20.4439738388089,
8.3914349759581));
#163643=CARTESIAN_POINT('Ctrl Pts',(-20.2627314453533,-20.4164862947188,
8.39378279081689));
#163644=CARTESIAN_POINT('Ctrl Pts',(-20.2676601582566,-20.4113239742267,
8.3942197195324));
#163645=CARTESIAN_POINT('Ctrl Pts',(-20.2753701279961,-20.4031663698583,
8.39490375109234));
#163646=CARTESIAN_POINT('Ctrl Pts',(-20.278168926037,-20.400187844515,8.39515217586332));
#163647=CARTESIAN_POINT('Ctrl Pts',(-20.2833998774868,-20.394588577113,
8.39561666395986));
#163648=CARTESIAN_POINT('Ctrl Pts',(-20.2858339895529,-20.3919698094932,
8.39583287430938));
#163649=CARTESIAN_POINT('Ctrl Pts',(-20.2913956837365,-20.3859557152884,
8.39632707339126));
#163650=CARTESIAN_POINT('Ctrl Pts',(-20.2945187973059,-20.3825563230121,
8.39660472123722));
#163651=CARTESIAN_POINT('Ctrl Pts',(-20.3041550132835,-20.3719985548134,
8.39746191207565));
#163652=CARTESIAN_POINT('Ctrl Pts',(-20.3106302724833,-20.36480559644,8.39803866294726));
#163653=CARTESIAN_POINT('Ctrl Pts',(-20.3791744960996,-20.2876059684725,
8.40415509886523));
#163654=CARTESIAN_POINT('Ctrl Pts',(-20.4365949716542,-20.2135931438384,
8.40937985143986));
#163655=CARTESIAN_POINT('Ctrl Pts',(-20.5627798944034,-20.0265630817037,
8.42175706785264));
#163656=CARTESIAN_POINT('Ctrl Pts',(-20.6262221693971,-19.910445244161,
8.42880643659293));
#163657=CARTESIAN_POINT('Ctrl Pts',(-20.7007281930072,-19.7373961374923,
8.43927197696545));
#163658=CARTESIAN_POINT('Ctrl Pts',(-20.7209425278633,-19.6847520627087,
8.442447726544));
#163659=CARTESIAN_POINT('Ctrl Pts',(-20.7502231670805,-19.5983354145247,
8.44769449782439));
#163660=CARTESIAN_POINT('Ctrl Pts',(-20.760596725774,-19.5650341201182,
8.44972403547661));
#163661=CARTESIAN_POINT('Ctrl Pts',(-20.7731190942457,-19.5210347587365,
8.45242173964668));
#163662=CARTESIAN_POINT('Ctrl Pts',(-20.7760149200363,-19.5105537546568,
8.45306553311528));
#163663=CARTESIAN_POINT('Ctrl Pts',(-20.7806193231252,-19.4933742952614,
8.45412288335269));
#163664=CARTESIAN_POINT('Ctrl Pts',(-20.7823760850546,-19.4866888756963,
8.45453487206151));
#163665=CARTESIAN_POINT('Ctrl Pts',(-20.7857090368825,-19.4737476843728,
8.45533342317431));
#163666=CARTESIAN_POINT('Ctrl Pts',(-20.7872894372081,-19.4674930686194,
8.45571984422475));
#163667=CARTESIAN_POINT('Ctrl Pts',(-20.7908666320066,-19.4530584371751,
8.45661277232929));
#163668=CARTESIAN_POINT('Ctrl Pts',(-20.7928432512142,-19.444873577154,
8.45711992420928));
#163669=CARTESIAN_POINT('Ctrl Pts',(-20.7980153370596,-19.4228826859008,
8.45848486374883));
#163670=CARTESIAN_POINT('Ctrl Pts',(-20.8011210529411,-19.4090561810748,
8.45934551768803));
#163671=CARTESIAN_POINT('Ctrl Pts',(-20.8354181895941,-19.2488618848786,
8.46934709518047));
#163672=CARTESIAN_POINT('Ctrl Pts',(-20.8511375064589,-19.0996426934846,
8.47899861842294));
#163673=CARTESIAN_POINT('Ctrl Pts',(-20.8508605238964,-18.8002697699751,
8.49872817936206));
#163674=CARTESIAN_POINT('Ctrl Pts',(-20.8348287879148,-18.6509266947224,
8.50874333683667));
#163675=CARTESIAN_POINT('Ctrl Pts',(-20.7998455024908,-18.4891628824865,
8.51906808111554));
#163676=CARTESIAN_POINT('Ctrl Pts',(-20.7963536193805,-18.4738437289619,
8.5200401730743));
#163677=CARTESIAN_POINT('Ctrl Pts',(-20.7913410447918,-18.452930476243,
8.52135814153985));
#163678=CARTESIAN_POINT('Ctrl Pts',(-20.7899675522461,-18.4473020803954,
8.52171194037775));
#163679=CARTESIAN_POINT('Ctrl Pts',(-20.7877485339626,-18.4383682263037,
8.52227199852567));
#163680=CARTESIAN_POINT('Ctrl Pts',(-20.7869181050291,-18.4350590999642,
8.52247911354343));
#163681=CARTESIAN_POINT('Ctrl Pts',(-20.7851867322695,-18.4282298288627,
8.52290584368497));
#163682=CARTESIAN_POINT('Ctrl Pts',(-20.7842847248074,-18.4247099942316,
8.52312539014692));
#163683=CARTESIAN_POINT('Ctrl Pts',(-20.7821142204911,-18.4163299804079,
8.52364718429002));
#163684=CARTESIAN_POINT('Ctrl Pts',(-20.7808374700019,-18.4114719224243,
8.52394895618862));
#163685=CARTESIAN_POINT('Ctrl Pts',(-20.7764750799278,-18.3951100607457,
8.52496302364301));
#163686=CARTESIAN_POINT('Ctrl Pts',(-20.7733095890909,-18.3836275243281,
8.52567085082336));
#163687=CARTESIAN_POINT('Ctrl Pts',(-20.7559961551047,-18.3228319585075,
8.52940111781873));
#163688=CARTESIAN_POINT('Ctrl Pts',(-20.740161981945,-18.2740393691834,
8.53233408680327));
#163689=CARTESIAN_POINT('Ctrl Pts',(-20.7225805426339,-18.2258895225534,
8.53521110136663));
#163690=CARTESIAN_POINT('Origin',(-18.734,-18.952,0.));
#163691=CARTESIAN_POINT('',(-20.7242503992901,-18.225264130614,9.55561792115202));
#163692=CARTESIAN_POINT('',(-20.7225805549386,-18.2258895562519,9.33206805306779));
#163693=CARTESIAN_POINT('',(-20.7225805737622,-18.2258896078036,0.));
#163694=CARTESIAN_POINT('',(-20.8516473698352,-18.9501064841217,9.51094372097752));
#163695=CARTESIAN_POINT('Ctrl Pts',(-20.8516473698352,-18.9501064841217,
9.51094372097752));
#163696=CARTESIAN_POINT('Ctrl Pts',(-20.8529700774227,-18.8071177722941,
9.51955279572483));
#163697=CARTESIAN_POINT('Ctrl Pts',(-20.8300641487808,-18.5602068596617,
9.53444419578299));
#163698=CARTESIAN_POINT('Ctrl Pts',(-20.7608945813314,-18.3228112333292,
9.54933559584116));
#163699=CARTESIAN_POINT('Ctrl Pts',(-20.7242503992901,-18.225264130614,
9.55561792115202));
#163700=CARTESIAN_POINT('Ctrl Pts',(-20.8509991358395,-18.9500871866797,
9.51057066838114));
#163701=CARTESIAN_POINT('Ctrl Pts',(-20.8511381041476,-19.1038898526281,
9.50220813078634));
#163702=CARTESIAN_POINT('Ctrl Pts',(-20.8345169833157,-19.2572409613586,
9.49391874038524));
#163703=CARTESIAN_POINT('Ctrl Pts',(-20.7961854588217,-19.4312433797309,
9.48368968190085));
#163704=CARTESIAN_POINT('Ctrl Pts',(-20.7905312722925,-19.4549534182221,
9.48227871564817));
#163705=CARTESIAN_POINT('Ctrl Pts',(-20.7813026756227,-19.4908903612793,
9.48011131877001));
#163706=CARTESIAN_POINT('Ctrl Pts',(-20.7780251063961,-19.5031918187829,
9.479364223302));
#163707=CARTESIAN_POINT('Ctrl Pts',(-20.7717280232907,-19.5259973356358,
9.47796915926823));
#163708=CARTESIAN_POINT('Ctrl Pts',(-20.768737719434,-19.5365090628525,
9.47732214536515));
#163709=CARTESIAN_POINT('Ctrl Pts',(-20.7637200154247,-19.5536424254093,
9.47626084521444));
#163710=CARTESIAN_POINT('Ctrl Pts',(-20.761741255831,-19.5602781820169,
9.47584814993044));
#163711=CARTESIAN_POINT('Ctrl Pts',(-20.75785750675,-19.573072742383,9.47504917587375));
#163712=CARTESIAN_POINT('Ctrl Pts',(-20.7559568686852,-19.5792327946707,
9.47466304349498));
#163713=CARTESIAN_POINT('Ctrl Pts',(-20.7515174988602,-19.5933911120992,
9.47377214713644));
#163714=CARTESIAN_POINT('Ctrl Pts',(-20.7489593002127,-19.6013831166627,
9.47326674770484));
#163715=CARTESIAN_POINT('Ctrl Pts',(-20.7419840095926,-19.6227363478494,
9.47190957728358));
#163716=CARTESIAN_POINT('Ctrl Pts',(-20.737481152593,-19.6360689199934,
9.47105499076286));
#163717=CARTESIAN_POINT('Ctrl Pts',(-20.6817078683167,-19.7959331739077,
9.46071961073483));
#163718=CARTESIAN_POINT('Ctrl Pts',(-20.6146125136166,-19.9364126033665,
9.45068614153466));
#163719=CARTESIAN_POINT('Ctrl Pts',(-20.4975435761416,-20.1250600647787,
9.43604111033634));
#163720=CARTESIAN_POINT('Ctrl Pts',(-20.4596328109739,-20.180147943552,
9.4316110303431));
#163721=CARTESIAN_POINT('Ctrl Pts',(-20.3826005136761,-20.2814576636098,
9.4232552919613));
#163722=CARTESIAN_POINT('Ctrl Pts',(-20.3439755690592,-20.3279800208125,
9.41932596895216));
#163723=CARTESIAN_POINT('Ctrl Pts',(-20.2831850000363,-20.395129591518,
9.41358312955422));
#163724=CARTESIAN_POINT('Ctrl Pts',(-20.2624837150291,-20.4170375189591,
9.41169737054865));
#163725=CARTESIAN_POINT('Ctrl Pts',(-20.2365531439382,-20.443331333503,
9.40942714190326));
#163726=CARTESIAN_POINT('Ctrl Pts',(-20.23176248186,-20.4481425892795,9.40901144210383));
#163727=CARTESIAN_POINT('Ctrl Pts',(-20.223992842341,-20.4558709090437,
9.40834335725904));
#163728=CARTESIAN_POINT('Ctrl Pts',(-20.2210282944535,-20.4588023206387,
9.40808986623123));
#163729=CARTESIAN_POINT('Ctrl Pts',(-20.2155127958052,-20.4642240390669,
9.40762091128048));
#163730=CARTESIAN_POINT('Ctrl Pts',(-20.2129642379326,-20.4667166374173,
9.40740527000457));
#163731=CARTESIAN_POINT('Ctrl Pts',(-20.20718628661,-20.4723392351493,9.40691873511417));
#163732=CARTESIAN_POINT('Ctrl Pts',(-20.2039532171942,-20.4754653803445,
9.40664814234676));
#163733=CARTESIAN_POINT('Ctrl Pts',(-20.1943749666198,-20.4846679810913,
9.40585125447342));
#163734=CARTESIAN_POINT('Ctrl Pts',(-20.1880018047704,-20.4907153541721,
9.40532716253214));
#163735=CARTESIAN_POINT('Ctrl Pts',(-20.1414361787023,-20.5343529410136,
9.40154057571614));
#163736=CARTESIAN_POINT('Ctrl Pts',(-20.0998255060236,-20.5704063838509,
9.39838604534943));
#163737=CARTESIAN_POINT('Ctrl Pts',(-20.0338650780997,-20.6231991996844,
9.3936413069055));
#163738=CARTESIAN_POINT('Ctrl Pts',(-20.0104948014801,-20.6411172572354,
9.39200641224539));
#163739=CARTESIAN_POINT('Ctrl Pts',(-19.8687657542256,-20.7451592964801,
9.38231535700458));
#163740=CARTESIAN_POINT('Ctrl Pts',(-19.7421104641031,-20.8193050860912,
9.37453712299876));
#163741=CARTESIAN_POINT('Ctrl Pts',(-19.5598230291656,-20.9020256416392,
9.36339458171594));
#163742=CARTESIAN_POINT('Ctrl Pts',(-19.5100026002917,-20.922381444268,
9.36035785293675));
#163743=CARTESIAN_POINT('Ctrl Pts',(-19.4279206572899,-20.9523225865046,
9.35532859778322));
#163744=CARTESIAN_POINT('Ctrl Pts',(-19.3961100711623,-20.9630759303931,
9.35337353151184));
#163745=CARTESIAN_POINT('Ctrl Pts',(-19.3537416006921,-20.9762841031516,
9.35075617822109));
#163746=CARTESIAN_POINT('Ctrl Pts',(-19.3434004072266,-20.9794212485368,
9.35011630906469));
#163747=CARTESIAN_POINT('Ctrl Pts',(-19.3264200364059,-20.9844308298599,
9.34906377043415));
#163748=CARTESIAN_POINT('Ctrl Pts',(-19.3197948436101,-20.9863502592151,
9.34865264127785));
#163749=CARTESIAN_POINT('Ctrl Pts',(-19.3069497415364,-20.9900037504982,
9.34785459005441));
#163750=CARTESIAN_POINT('Ctrl Pts',(-19.3007310394531,-20.9917418024982,
9.34746780314688));
#163751=CARTESIAN_POINT('Ctrl Pts',(-19.286350308711,-20.9956902016434,
9.3465723334617));
#163752=CARTESIAN_POINT('Ctrl Pts',(-19.2781828346788,-20.9978801389687,
9.34606299413454));
#163753=CARTESIAN_POINT('Ctrl Pts',(-19.2561739646419,-21.0036402411046,
9.34468833531461));
#163754=CARTESIAN_POINT('Ctrl Pts',(-19.2423093518582,-21.0071191973585,
9.34382008543131));
#163755=CARTESIAN_POINT('Ctrl Pts',(-19.1144643894697,-21.0378256544474,
9.33579182406495));
#163756=CARTESIAN_POINT('Ctrl Pts',(-18.9984611491077,-21.0556811168636,
9.32832819637869));
#163757=CARTESIAN_POINT('Ctrl Pts',(-18.7181701751453,-21.075270069993,
9.30997281786804));
#163758=CARTESIAN_POINT('Ctrl Pts',(-18.5539784407095,-21.0676840157774,
9.29893810294639));
#163759=CARTESIAN_POINT('Ctrl Pts',(-18.361482832506,-21.0362013693955,
9.28655902439747));
#163760=CARTESIAN_POINT('Ctrl Pts',(-18.3307745008561,-21.0304787285515,
9.28460334716877));
#163761=CARTESIAN_POINT('Ctrl Pts',(-18.2932036206526,-21.0226131168049,
9.28224337530656));
#163762=CARTESIAN_POINT('Ctrl Pts',(-18.2862123482478,-21.0211124546123,
9.28180563118817));
#163763=CARTESIAN_POINT('Ctrl Pts',(-18.2752341694001,-21.0186977623501,
9.28112061096522));
#163764=CARTESIAN_POINT('Ctrl Pts',(-18.2712421548218,-21.01780756742,9.28087200670439));
#163765=CARTESIAN_POINT('Ctrl Pts',(-18.263765793451,-21.0161176252269,
9.2804073665353));
#163766=CARTESIAN_POINT('Ctrl Pts',(-18.2602809326335,-21.0153206307328,
9.28019118251321));
#163767=CARTESIAN_POINT('Ctrl Pts',(-18.2523051187396,-21.0134752747015,
9.27969728310955));
#163768=CARTESIAN_POINT('Ctrl Pts',(-18.2478155691192,-21.0124210654451,
9.27941990707483));
#163769=CARTESIAN_POINT('Ctrl Pts',(-18.2360631289159,-21.0096208759835,
9.27869539730786));
#163770=CARTESIAN_POINT('Ctrl Pts',(-18.2288058989922,-21.0078510940494,
9.27824959650462));
#163771=CARTESIAN_POINT('Ctrl Pts',(-18.1802070805174,-20.9957266771959,
9.27527398984196));
#163772=CARTESIAN_POINT('Ctrl Pts',(-18.1391738450166,-20.9841633118678,
9.27280893696925));
#163773=CARTESIAN_POINT('Ctrl Pts',(-18.0895913035468,-20.9685599285352,
9.26985736773424));
#163774=CARTESIAN_POINT('Ctrl Pts',(-18.0806864686085,-20.9656926149575,
9.26932835920203));
#163775=CARTESIAN_POINT('Ctrl Pts',(-18.0582615546534,-20.9583074905242,
9.2679982349122));
#163776=CARTESIAN_POINT('Ctrl Pts',(-18.0447674411228,-20.9537119388753,
9.26719974487325));
#163777=CARTESIAN_POINT('Ctrl Pts',(-17.8963683822808,-20.9014946163468,
9.2584294569468));
#163778=CARTESIAN_POINT('Ctrl Pts',(-17.7665730417788,-20.840450405558,
9.25083404290633));
#163779=CARTESIAN_POINT('Ctrl Pts',(-17.5642102998977,-20.7188977232798,
9.23783370955003));
#163780=CARTESIAN_POINT('Ctrl Pts',(-17.4877481080449,-20.6658228708152,
9.23261305367473));
#163781=CARTESIAN_POINT('Ctrl Pts',(-17.3985207912997,-20.5947506203344,
9.22596857980004));
#163782=CARTESIAN_POINT('Ctrl Pts',(-17.3822125405451,-20.5813572151364,
9.22473009213701));
#163783=CARTESIAN_POINT('Ctrl Pts',(-17.3592686770775,-20.5619326337178,
9.22295165380776));
#163784=CARTESIAN_POINT('Ctrl Pts',(-17.3524666128674,-20.5560993709279,
9.22241979314118));
#163785=CARTESIAN_POINT('Ctrl Pts',(-17.3407814593065,-20.5459490507351,
9.22149800089068));
#163786=CARTESIAN_POINT('Ctrl Pts',(-17.3358808597868,-20.5416522722835,
9.22110891354562));
#163787=CARTESIAN_POINT('Ctrl Pts',(-17.3265256691613,-20.5333730460088,
9.2203612998821));
#163788=CARTESIAN_POINT('Ctrl Pts',(-17.3220679377208,-20.5293942287784,
9.220002927831));
#163789=CARTESIAN_POINT('Ctrl Pts',(-17.3104982747064,-20.5189792092125,
9.21906718185095));
#163790=CARTESIAN_POINT('Ctrl Pts',(-17.3034131946583,-20.5125135025574,
9.21848856323691));
#163791=CARTESIAN_POINT('Ctrl Pts',(-17.279292035105,-20.4901986724106,
9.21649923682406));
#163792=CARTESIAN_POINT('Ctrl Pts',(-17.2624739176394,-20.4741173870864,
9.21507861821106));
#163793=CARTESIAN_POINT('Ctrl Pts',(-17.1239722440033,-20.3372426230275,
9.20308976205596));
#163794=CARTESIAN_POINT('Ctrl Pts',(-17.0171345894265,-20.2023750407871,
9.19185378569772));
#163795=CARTESIAN_POINT('Ctrl Pts',(-16.8808718570458,-19.9794635054932,
9.17458946507389));
#163796=CARTESIAN_POINT('Ctrl Pts',(-16.8389276933185,-19.8998755760097,
9.16865950876779));
#163797=CARTESIAN_POINT('Ctrl Pts',(-16.7864056199242,-19.7826925966121,
9.16045580284078));
#163798=CARTESIAN_POINT('Ctrl Pts',(-16.7716060658502,-19.7471003323287,
9.15803060990445));
#163799=CARTESIAN_POINT('Ctrl Pts',(-16.7550559687385,-19.7040156008535,
9.15519024756636));
#163800=CARTESIAN_POINT('Ctrl Pts',(-16.7523647218982,-19.6968950069744,
9.15472389814967));
#163801=CARTESIAN_POINT('Ctrl Pts',(-16.7482513643726,-19.6858316703895,
9.1540042591649));
#163802=CARTESIAN_POINT('Ctrl Pts',(-16.746802488259,-19.6818990439752,
9.1537494151912));
#163803=CARTESIAN_POINT('Ctrl Pts',(-16.7441434536272,-19.6746151257614,
9.15327921241018));
#163804=CARTESIAN_POINT('Ctrl Pts',(-16.7429300871859,-19.6712651094804,
9.15306366828498));
#163805=CARTESIAN_POINT('Ctrl Pts',(-16.7402139558944,-19.663706526441,
9.15257893036685));
#163806=CARTESIAN_POINT('Ctrl Pts',(-16.7387160599745,-19.6594962678115,
9.15231002778688));
#163807=CARTESIAN_POINT('Ctrl Pts',(-16.734356889319,-19.6471196337873,
9.15152270458673));
#163808=CARTESIAN_POINT('Ctrl Pts',(-16.73153229896,-19.6389403085139,9.15100640896423));
#163809=CARTESIAN_POINT('Ctrl Pts',(-16.7121496273789,-19.5816772396143,
9.14741837822285));
#163810=CARTESIAN_POINT('Ctrl Pts',(-16.6973463967351,-19.5320132733231,
9.14444217897079));
#163811=CARTESIAN_POINT('Ctrl Pts',(-16.6790027014076,-19.4610545598867,
9.14031504517448));
#163812=CARTESIAN_POINT('Ctrl Pts',(-16.6739430224537,-19.4401759260615,
9.1391157729302));
#163813=CARTESIAN_POINT('Ctrl Pts',(-16.6387826487345,-19.284791865949,
9.13027867056794));
#163814=CARTESIAN_POINT('Ctrl Pts',(-16.6215637283688,-19.147708582813,
9.12294817445163));
#163815=CARTESIAN_POINT('Ctrl Pts',(-16.615309099425,-18.9191858084987,
9.11034446304863));
#163816=CARTESIAN_POINT('Ctrl Pts',(-16.6186638528939,-18.8283951773765,
9.10524206797293));
#163817=CARTESIAN_POINT('Ctrl Pts',(-16.6299380705484,-18.7173803260278,
9.0987406747198));
#163818=CARTESIAN_POINT('Ctrl Pts',(-16.6323486712366,-18.6966871702582,
9.09751780252641));
#163819=CARTESIAN_POINT('Ctrl Pts',(-16.6362262763969,-18.6671950257068,
9.09575791970911));
#163820=CARTESIAN_POINT('Ctrl Pts',(-16.6374441524653,-18.6583640974157,
9.09522876664305));
#163821=CARTESIAN_POINT('Ctrl Pts',(-16.6396477465044,-18.6430987063396,
9.09431017162974));
#163822=CARTESIAN_POINT('Ctrl Pts',(-16.6406074397981,-18.6366605664067,
9.09392155796625));
#163823=CARTESIAN_POINT('Ctrl Pts',(-16.6425065312993,-18.6243112852303,
9.09317379951298));
#163824=CARTESIAN_POINT('Ctrl Pts',(-16.643441336852,-18.618399493108,9.09281480392395));
#163825=CARTESIAN_POINT('Ctrl Pts',(-16.6459483158343,-18.6029695854948,
9.09187508268392));
#163826=CARTESIAN_POINT('Ctrl Pts',(-16.6475604889846,-18.5934581920447,
9.09129309150555));
#163827=CARTESIAN_POINT('Ctrl Pts',(-16.6533404890244,-18.560717538348,
9.0892801540355));
#163828=CARTESIAN_POINT('Ctrl Pts',(-16.6578315864026,-18.5375478157145,
9.08783897823118));
#163829=CARTESIAN_POINT('Ctrl Pts',(-16.6968556528412,-18.352810501556,
9.07621020717517));
#163830=CARTESIAN_POINT('Ctrl Pts',(-16.7498017832939,-18.1957441785992,
9.06540809439343));
#163831=CARTESIAN_POINT('Ctrl Pts',(-16.8749495067224,-17.9312866457703,
9.04607356575698));
#163832=CARTESIAN_POINT('Ctrl Pts',(-16.9397450201553,-17.8212567516476,
9.03764617730179));
#163833=CARTESIAN_POINT('Ctrl Pts',(-17.0210404729426,-17.7079733055976,
9.02899840108267));
#163834=CARTESIAN_POINT('Ctrl Pts',(-17.0281138238902,-17.6982914504789,
9.02825969768888));
#163835=CARTESIAN_POINT('Ctrl Pts',(-17.0382747907705,-17.6846285544052,
9.02721841419493));
#163836=CARTESIAN_POINT('Ctrl Pts',(-17.0412947946315,-17.680597838901,
9.0269113689375));
#163837=CARTESIAN_POINT('Ctrl Pts',(-17.0465196874146,-17.6736759353483,
9.0263843907951));
#163838=CARTESIAN_POINT('Ctrl Pts',(-17.0487176834492,-17.6707795919789,
9.02616398035468));
#163839=CARTESIAN_POINT('Ctrl Pts',(-17.0529903633942,-17.6651794157292,
9.02573801159993));
#163840=CARTESIAN_POINT('Ctrl Pts',(-17.0550641144242,-17.6624749296854,
9.02553238808375));
#163841=CARTESIAN_POINT('Ctrl Pts',(-17.0606692307923,-17.6552014487085,
9.02497958632524));
#163842=CARTESIAN_POINT('Ctrl Pts',(-17.0642128045286,-17.6506418366078,
9.02463326373037));
#163843=CARTESIAN_POINT('Ctrl Pts',(-17.0773899393621,-17.6338288985197,
9.02335682177934));
#163844=CARTESIAN_POINT('Ctrl Pts',(-17.087140349686,-17.6216672334073,
9.02243464057827));
#163845=CARTESIAN_POINT('Ctrl Pts',(-17.1836987557838,-17.5039188801019,
9.01350504256178));
#163846=CARTESIAN_POINT('Ctrl Pts',(-17.2804185889484,-17.4068513557522,
9.00612170206973));
#163847=CARTESIAN_POINT('Ctrl Pts',(-17.504977073461,-17.2213728878404,
8.99030511144564));
#163848=CARTESIAN_POINT('Ctrl Pts',(-17.6345175939576,-17.1363187132246,
8.98188562765167));
#163849=CARTESIAN_POINT('Ctrl Pts',(-17.7911005486999,-17.0564573234692,
8.97164911556871));
#163850=CARTESIAN_POINT('Ctrl Pts',(-17.8101924711805,-17.0470797877685,
8.97040094469934));
#163851=CARTESIAN_POINT('Ctrl Pts',(-17.8375492459361,-17.0341507222992,
8.96861100998308));
#163852=CARTESIAN_POINT('Ctrl Pts',(-17.8457008240836,-17.0303615385017,
8.96807748196929));
#163853=CARTESIAN_POINT('Ctrl Pts',(-17.8598084666157,-17.0239126813327,
8.96715371755052));
#163854=CARTESIAN_POINT('Ctrl Pts',(-17.8657531888928,-17.0212283876698,
8.96676433523984));
#163855=CARTESIAN_POINT('Ctrl Pts',(-17.8771616918953,-17.0161403087556,
8.96601679682546));
#163856=CARTESIAN_POINT('Ctrl Pts',(-17.8826234277886,-17.0137320717775,
8.96565879807748));
#163857=CARTESIAN_POINT('Ctrl Pts',(-17.8968576469632,-17.007527565476,
8.96472544240179));
#163858=CARTESIAN_POINT('Ctrl Pts',(-17.905645714064,-17.0037675856932,
8.96414885327789));
#163859=CARTESIAN_POINT('Ctrl Pts',(-17.9357273911675,-16.9911374510831,
8.96217383329906));
#163860=CARTESIAN_POINT('Ctrl Pts',(-17.9571397857485,-16.9825561101635,
8.96076568283578));
#163861=CARTESIAN_POINT('Ctrl Pts',(-18.1416936516153,-16.9120713442594,
8.9486048803617));
#163862=CARTESIAN_POINT('Ctrl Pts',(-18.3117422850142,-16.8702192482116,
8.93715757058177));
#163863=CARTESIAN_POINT('Ctrl Pts',(-18.5720581959768,-16.8393814125528,
8.9198371751882));
#163864=CARTESIAN_POINT('Ctrl Pts',(-18.6597241630551,-16.8344855422463,
8.91405468550886));
#163865=CARTESIAN_POINT('Ctrl Pts',(-18.7854445872254,-16.8352840464526,
8.9060266176787));
#163866=CARTESIAN_POINT('Ctrl Pts',(-18.8234329098846,-16.836548477608,
8.90363605743844));
#163867=CARTESIAN_POINT('Ctrl Pts',(-18.8689372456965,-16.8392912118718,
8.90083077414067));
#163868=CARTESIAN_POINT('Ctrl Pts',(-18.876502939195,-16.8397880314644,
8.90036629757931));
#163869=CARTESIAN_POINT('Ctrl Pts',(-18.888239837257,-16.8406221129123,
8.89964892102637));
#163870=CARTESIAN_POINT('Ctrl Pts',(-18.8924128972011,-16.8409311086135,
8.89939448190194));
#163871=CARTESIAN_POINT('Ctrl Pts',(-18.9001380751228,-16.841526157744,
8.89892465470663));
#163872=CARTESIAN_POINT('Ctrl Pts',(-18.9036903565058,-16.8418088043824,
8.89870908369598));
#163873=CARTESIAN_POINT('Ctrl Pts',(-18.9117040926966,-16.8424668051863,
8.89822381799846));
#163874=CARTESIAN_POINT('Ctrl Pts',(-18.9161650676632,-16.8428473422836,
8.8979544173659));
#163875=CARTESIAN_POINT('Ctrl Pts',(-18.9292829715273,-16.844008275337,
8.89716428121397));
#163876=CARTESIAN_POINT('Ctrl Pts',(-18.9379364610857,-16.8448278485328,
8.8966456935359));
#163877=CARTESIAN_POINT('Ctrl Pts',(-18.999056550301,-16.8509965841484,
8.89300001592043));
#163878=CARTESIAN_POINT('Ctrl Pts',(-19.0513168421041,-16.8582518445311,
8.88997199161438));
#163879=CARTESIAN_POINT('Ctrl Pts',(-19.1188003152317,-16.8702058393252,
8.88611580285936));
#163880=CARTESIAN_POINT('Ctrl Pts',(-19.1343136997619,-16.873133200655,
8.88523307620626));
#163881=CARTESIAN_POINT('Ctrl Pts',(-19.199644025459,-16.8862194061496,
8.88152631588851));
#163882=CARTESIAN_POINT('Ctrl Pts',(-19.2491207459418,-16.8979978613761,
8.87874487186873));
#163883=CARTESIAN_POINT('Ctrl Pts',(-19.4035796536921,-16.940701321278,
8.87001970660592));
#163884=CARTESIAN_POINT('Ctrl Pts',(-19.5066126375289,-16.9779867976233,
8.86412872711329));
#163885=CARTESIAN_POINT('Ctrl Pts',(-19.6565774913472,-17.0458035922493,
8.85497767308567));
#163886=CARTESIAN_POINT('Ctrl Pts',(-19.7059453799687,-17.0704964779932,
8.85186630565953));
#163887=CARTESIAN_POINT('Ctrl Pts',(-19.7843784777631,-17.1136384256498,
8.84671648862589));
#163888=CARTESIAN_POINT('Ctrl Pts',(-19.8140584803238,-17.1309174355497,
8.84471754338035));
#163889=CARTESIAN_POINT('Ctrl Pts',(-19.8525132559002,-17.1545757292901,
8.84205479995177));
#163890=CARTESIAN_POINT('Ctrl Pts',(-19.8616788922531,-17.1603119071771,
8.84141457744484));
#163891=CARTESIAN_POINT('Ctrl Pts',(-19.876619979032,-17.1698226296123,
8.84036160564818));
#163892=CARTESIAN_POINT('Ctrl Pts',(-19.8824217030079,-17.1735556836569,
8.83995039916686));
#163893=CARTESIAN_POINT('Ctrl Pts',(-19.8936175179121,-17.1808371337984,
8.83915230365066));
#163894=CARTESIAN_POINT('Ctrl Pts',(-19.8990138327789,-17.184381982876,
8.83876555033536));
#163895=CARTESIAN_POINT('Ctrl Pts',(-19.9114372705261,-17.192624564624,
8.83787031252863));
#163896=CARTESIAN_POINT('Ctrl Pts',(-19.9184526071277,-17.1973397859244,
8.83736117255716));
#163897=CARTESIAN_POINT('Ctrl Pts',(-19.9372457725075,-17.2101353045223,
8.83598740051634));
#163898=CARTESIAN_POINT('Ctrl Pts',(-19.9489702181702,-17.2182928852677,
8.83511984393464));
#163899=CARTESIAN_POINT('Ctrl Pts',(-20.0755780804865,-17.3082985336551,
8.82563486559488));
#163900=CARTESIAN_POINT('Ctrl Pts',(-20.1820673903348,-17.4012989519405,
8.81656774780422));
#163901=CARTESIAN_POINT('Ctrl Pts',(-20.3445946017893,-17.5746792090217,
8.80093336788623));
#163902=CARTESIAN_POINT('Ctrl Pts',(-20.4057792782527,-17.6496245639738,
8.79450519601258));
#163903=CARTESIAN_POINT('Ctrl Pts',(-20.4993339368746,-17.7817261076463,
8.78394205739131));
#163904=CARTESIAN_POINT('Ctrl Pts',(-20.5345603061946,-17.8366842997629,
8.77974793333697));
#163905=CARTESIAN_POINT('Ctrl Pts',(-20.5737749643587,-17.9045792771297,
8.77487649203968));
#163906=CARTESIAN_POINT('Ctrl Pts',(-20.58024894635,-17.9160333314806,8.77406490345128));
#163907=CARTESIAN_POINT('Ctrl Pts',(-20.5891459494667,-17.9321226344458,
8.77293990512952));
#163908=CARTESIAN_POINT('Ctrl Pts',(-20.5916590625786,-17.9367073608292,
8.7726210204753));
#163909=CARTESIAN_POINT('Ctrl Pts',(-20.595907905499,-17.9445272067099,
8.77208005258767));
#163910=CARTESIAN_POINT('Ctrl Pts',(-20.5976522428747,-17.947757600909,
8.77185742524005));
#163911=CARTESIAN_POINT('Ctrl Pts',(-20.6009776731519,-17.9539545762238,
8.77143199582076));
#163912=CARTESIAN_POINT('Ctrl Pts',(-20.6025601087192,-17.9569203949248,
8.77122910564776));
#163913=CARTESIAN_POINT('Ctrl Pts',(-20.6067291654024,-17.9647791009159,
8.77069335629071));
#163914=CARTESIAN_POINT('Ctrl Pts',(-20.609303695573,-17.969678422573,8.77036125971394));
#163915=CARTESIAN_POINT('Ctrl Pts',(-20.618348793068,-17.9870563708885,
8.76918983413319));
#163916=CARTESIAN_POINT('Ctrl Pts',(-20.6247144223299,-17.999589595726,
8.76835685001149));
#163917=CARTESIAN_POINT('Ctrl Pts',(-20.6654151825277,-18.0817414688069,
8.76296784094099));
#163918=CARTESIAN_POINT('Ctrl Pts',(-20.6959972252147,-18.1530864111672,
8.75861684946317));
#163919=CARTESIAN_POINT('Ctrl Pts',(-20.7225806939367,-18.2258899369226,
8.75434681593714));
#163920=CARTESIAN_POINT('',(-20.8509999019998,-18.9526441527879,9.29097295163941));
#163921=CARTESIAN_POINT('Ctrl Pts',(-20.7225805426339,-18.2258895225534,
8.53521110136663));
#163922=CARTESIAN_POINT('Ctrl Pts',(-20.6972665242699,-18.1565626557224,
8.53935346981564));
#163923=CARTESIAN_POINT('Ctrl Pts',(-20.6683303334796,-18.0885682846539,
8.54338079649807));
#163924=CARTESIAN_POINT('Ctrl Pts',(-20.5622083440441,-17.8715011606762,
8.55651370999459));
#163925=CARTESIAN_POINT('Ctrl Pts',(-20.4709010471761,-17.7301197687966,
8.56556717419578));
#163926=CARTESIAN_POINT('Ctrl Pts',(-20.3488895493943,-17.5829229611688,
8.57667158329379));
#163927=CARTESIAN_POINT('Ctrl Pts',(-20.3336077518508,-17.5650987164041,
8.57804658318816));
#163928=CARTESIAN_POINT('Ctrl Pts',(-20.3116465924116,-17.5403297476765,
8.58000258058673));
#163929=CARTESIAN_POINT('Ctrl Pts',(-20.3052110916489,-17.5331704215547,
8.58057342378957));
#163930=CARTESIAN_POINT('Ctrl Pts',(-20.2946981030954,-17.5216342392475,
8.58150230232897));
#163931=CARTESIAN_POINT('Ctrl Pts',(-20.2906504545105,-17.5172302833276,
8.58185907151936));
#163932=CARTESIAN_POINT('Ctrl Pts',(-20.2821570953286,-17.5080675159734,
8.58260593747009));
#163933=CARTESIAN_POINT('Ctrl Pts',(-20.2777079871463,-17.5033119524227,
8.58299617765471));
#163934=CARTESIAN_POINT('Ctrl Pts',(-20.2671051351112,-17.4920830789144,
8.58392387591232));
#163935=CARTESIAN_POINT('Ctrl Pts',(-20.2609322647377,-17.4856280734894,
8.58446215778479));
#163936=CARTESIAN_POINT('Ctrl Pts',(-20.2401569148386,-17.4641765992511,
8.58626791079944));
#163937=CARTESIAN_POINT('Ctrl Pts',(-20.2253732608154,-17.4493580361652,
8.58754329127387));
#163938=CARTESIAN_POINT('Ctrl Pts',(-20.1447383747647,-17.3708949945944,
8.59445101743442));
#163939=CARTESIAN_POINT('Ctrl Pts',(-20.0750376008408,-17.3113628780678,
8.60025767198204));
#163940=CARTESIAN_POINT('Ctrl Pts',(-19.9260794546773,-17.1999859093171,
8.61232141509067));
#163941=CARTESIAN_POINT('Ctrl Pts',(-19.8467532513525,-17.1485629253094,
8.61857370208974));
#163942=CARTESIAN_POINT('Ctrl Pts',(-19.69941499979,-17.0664832361175,8.62971091800337));
#163943=CARTESIAN_POINT('Ctrl Pts',(-19.6327063508674,-17.033790487146,
8.63459304918896));
#163944=CARTESIAN_POINT('Ctrl Pts',(-19.5255532143106,-16.9880963979304,
8.64206175425803));
#163945=CARTESIAN_POINT('Ctrl Pts',(-19.4862012034366,-16.9726900820359,
8.64472886806517));
#163946=CARTESIAN_POINT('Ctrl Pts',(-19.4393956540965,-16.9559635572666,
8.64779175402888));
#163947=CARTESIAN_POINT('Ctrl Pts',(-19.4323664130114,-16.953493340899,
8.64824887347503));
#163948=CARTESIAN_POINT('Ctrl Pts',(-19.4209708582735,-16.9495561797331,
8.64898514491787));
#163949=CARTESIAN_POINT('Ctrl Pts',(-19.4166126125074,-16.9480663095767,
8.64926560284719));
#163950=CARTESIAN_POINT('Ctrl Pts',(-19.4088636488684,-16.9454455325902,
8.64976220818604));
#163951=CARTESIAN_POINT('Ctrl Pts',(-19.4054748993097,-16.944308979072,
8.64997868581606));
#163952=CARTESIAN_POINT('Ctrl Pts',(-19.3981986904133,-16.9418890930745,
8.6504419979075));
#163953=CARTESIAN_POINT('Ctrl Pts',(-19.3943103934574,-16.9406084559607,
8.65068867293238));
#163954=CARTESIAN_POINT('Ctrl Pts',(-19.3836044849367,-16.937116782336,
8.65136541617538));
#163955=CARTESIAN_POINT('Ctrl Pts',(-19.3767792490089,-16.9349290522986,
8.65179413359938));
#163956=CARTESIAN_POINT('Ctrl Pts',(-19.3399295280785,-16.9233234458084,
8.65409481638683));
#163957=CARTESIAN_POINT('Ctrl Pts',(-19.3097072852235,-16.9145406716367,
8.65593182017731));
#163958=CARTESIAN_POINT('Ctrl Pts',(-19.1212225674714,-16.86429516803,8.66714519059627));
#163959=CARTESIAN_POINT('Ctrl Pts',(-18.9587779967234,-16.8406165954596,
8.67579052725774));
#163960=CARTESIAN_POINT('Ctrl Pts',(-18.6781394616569,-16.832498599573,
8.69115902284257));
#163961=CARTESIAN_POINT('Ctrl Pts',(-18.5610028698173,-16.8388333500567,
8.69769648655017));
#163962=CARTESIAN_POINT('Ctrl Pts',(-18.4308397096218,-16.8567703827533,
8.70539390519138));
#163963=CARTESIAN_POINT('Ctrl Pts',(-18.4167001908331,-16.8588650003329,
8.70623563542497));
#163964=CARTESIAN_POINT('Ctrl Pts',(-18.3942316636953,-16.8624263644267,
8.70758250453314));
#163965=CARTESIAN_POINT('Ctrl Pts',(-18.3858882073737,-16.8638001346833,
8.70808470020775));
#163966=CARTESIAN_POINT('Ctrl Pts',(-18.3711884697787,-16.866311028332,
8.70897318841858));
#163967=CARTESIAN_POINT('Ctrl Pts',(-18.3648287057149,-16.8674273226751,
8.70935881456289));
#163968=CARTESIAN_POINT('Ctrl Pts',(-18.3516858596697,-16.8697962451304,
8.71015831432772));
#163969=CARTESIAN_POINT('Ctrl Pts',(-18.3449036013917,-16.8710529633054,
8.71057231412069));
#163970=CARTESIAN_POINT('Ctrl Pts',(-18.3275114001116,-16.8743636489613,
8.71163767683571));
#163971=CARTESIAN_POINT('Ctrl Pts',(-18.3169109201649,-16.8764657358413,
8.71229056844244));
#163972=CARTESIAN_POINT('Ctrl Pts',(-18.2727439827485,-16.8855761077512,
8.71502600536989));
#163973=CARTESIAN_POINT('Ctrl Pts',(-18.2393357382228,-16.8933179293513,
8.71713186872803));
#163974=CARTESIAN_POINT('Ctrl Pts',(-18.1527992824592,-16.9155993415684,
8.72268614556567));
#163975=CARTESIAN_POINT('Ctrl Pts',(-18.100026993056,-16.9314061955281,
8.72617294103055));
#163976=CARTESIAN_POINT('Ctrl Pts',(-17.9444687753924,-16.9846945372803,
8.73674191965459));
#163977=CARTESIAN_POINT('Ctrl Pts',(-17.8439124925375,-17.0281000283955,
8.74397249551155));
#163978=CARTESIAN_POINT('Ctrl Pts',(-17.7067694966179,-17.100359753312,
8.75421242629077));
#163979=CARTESIAN_POINT('Ctrl Pts',(-17.6670694038645,-17.1229474026885,
8.75722324029487));
#163980=CARTESIAN_POINT('Ctrl Pts',(-17.6086454621591,-17.1587380864235,
8.76169862425411));
#163981=CARTESIAN_POINT('Ctrl Pts',(-17.5893548707656,-17.1709894140694,
8.76318384235468));
#163982=CARTESIAN_POINT('Ctrl Pts',(-17.5696699074774,-17.1839431726464,
8.76470463059978));
#163983=CARTESIAN_POINT('Ctrl Pts',(-17.5690740650417,-17.1843357006578,
8.76475066816479));
#163984=CARTESIAN_POINT('Ctrl Pts',(-17.5588413988646,-17.1910841790031,
8.76554137549075));
#163985=CARTESIAN_POINT('Ctrl Pts',(-17.5492563645857,-17.1975186539752,
8.76628331708627));
#163986=CARTESIAN_POINT('Ctrl Pts',(-17.5067680482133,-17.2265482153437,
8.76957635694986));
#163987=CARTESIAN_POINT('Ctrl Pts',(-17.4744526720219,-17.2499943813663,
8.77209231810606));
#163988=CARTESIAN_POINT('Ctrl Pts',(-17.4370127209066,-17.2788094399821,
8.7750028301279));
#163989=CARTESIAN_POINT('Ctrl Pts',(-17.4312311912743,-17.2833070723325,
8.77545214324752));
#163990=CARTESIAN_POINT('Ctrl Pts',(-17.4218822397499,-17.2906581180568,
8.77617832313805));
#163991=CARTESIAN_POINT('Ctrl Pts',(-17.4183005616039,-17.2934931853711,
8.77645643948385));
#163992=CARTESIAN_POINT('Ctrl Pts',(-17.4119355667385,-17.2985649745377,
8.77695047475222));
#163993=CARTESIAN_POINT('Ctrl Pts',(-17.4091487116816,-17.3007971615793,
8.77716671091171));
#163994=CARTESIAN_POINT('Ctrl Pts',(-17.4031593394883,-17.3056193939515,
8.77763127042905));
#163995=CARTESIAN_POINT('Ctrl Pts',(-17.3999587389038,-17.3082117295707,
8.7778794250553));
#163996=CARTESIAN_POINT('Ctrl Pts',(-17.3911214010762,-17.3154123680795,
8.77856441327161));
#163997=CARTESIAN_POINT('Ctrl Pts',(-17.3855007783683,-17.3200404842148,
8.77899984091943));
#163998=CARTESIAN_POINT('Ctrl Pts',(-17.3544490049284,-17.3458790008428,
8.78140483755214));
#163999=CARTESIAN_POINT('Ctrl Pts',(-17.3294928417276,-17.3676561201549,
8.78333558814122));
#164000=CARTESIAN_POINT('Ctrl Pts',(-17.1853821468889,-17.4994919240165,
8.79454282715386));
#164001=CARTESIAN_POINT('Ctrl Pts',(-17.0786739900886,-17.6223743399111,
8.80311685693869));
#164002=CARTESIAN_POINT('Ctrl Pts',(-16.9211382245734,-17.8525301244748,
8.81838643560507));
#164003=CARTESIAN_POINT('Ctrl Pts',(-16.8633175490734,-17.954080290613,
8.82490033117783));
#164004=CARTESIAN_POINT('Ctrl Pts',(-16.8081379465477,-18.0728251063192,
8.83257121970849));
#164005=CARTESIAN_POINT('Ctrl Pts',(-16.8022482983483,-18.085842686997,
8.83341260847234));
#164006=CARTESIAN_POINT('Ctrl Pts',(-16.7930842465057,-18.1066559813539,
8.83475903324848));
#164007=CARTESIAN_POINT('Ctrl Pts',(-16.789723934019,-18.1144135578259,
8.835261129134));
#164008=CARTESIAN_POINT('Ctrl Pts',(-16.7838793432726,-18.1281310094465,
8.83614950110599));
#164009=CARTESIAN_POINT('Ctrl Pts',(-16.7813756822984,-18.1340825457999,
8.8365351113601));
#164010=CARTESIAN_POINT('Ctrl Pts',(-16.7762534857181,-18.1464162526112,
8.83733463740967));
#164011=CARTESIAN_POINT('Ctrl Pts',(-16.7736388436888,-18.1527999478767,
8.83774867966963));
#164012=CARTESIAN_POINT('Ctrl Pts',(-16.7670071750608,-18.1692196452377,
8.83881427643071));
#164013=CARTESIAN_POINT('Ctrl Pts',(-16.7630357701188,-18.1792737516399,
8.83946736091313));
#164014=CARTESIAN_POINT('Ctrl Pts',(-16.7467787879333,-18.221371124696,
8.84220466712063));
#164015=CARTESIAN_POINT('Ctrl Pts',(-16.7351968440456,-18.2536788515808,
8.84431224676059));
#164016=CARTESIAN_POINT('Ctrl Pts',(-16.7070678086544,-18.3385878264479,
8.84987212998108));
#164017=CARTESIAN_POINT('Ctrl Pts',(-16.691782216499,-18.3915766728047,
8.85336291221959));
#164018=CARTESIAN_POINT('Ctrl Pts',(-16.6523833652625,-18.5513336122024,
8.86393954887878));
#164019=CARTESIAN_POINT('Ctrl Pts',(-16.6344613551274,-18.6594331156954,
8.87117377045224));
#164020=CARTESIAN_POINT('Ctrl Pts',(-16.6206253038515,-18.8183891045912,
8.88171361671619));
#164021=CARTESIAN_POINT('Ctrl Pts',(-16.6180530156316,-18.8684948705913,
8.88501984760389));
#164022=CARTESIAN_POINT('Ctrl Pts',(-16.617005625155,-18.9349649137186,
8.88935317982335));
#164023=CARTESIAN_POINT('Ctrl Pts',(-16.6169372026051,-18.9512866916918,
8.89041298416674));
#164024=CARTESIAN_POINT('Ctrl Pts',(-16.6174479434466,-19.0205597976937,
8.89488902191761));
#164025=CARTESIAN_POINT('Ctrl Pts',(-16.6198250184815,-19.0734834067384,
8.89825443247823));
#164026=CARTESIAN_POINT('Ctrl Pts',(-16.6249008382123,-19.1349354757757,
8.90205801412985));
#164027=CARTESIAN_POINT('Ctrl Pts',(-16.6256703084449,-19.1436000527463,
8.90259188014106));
#164028=CARTESIAN_POINT('Ctrl Pts',(-16.6269168264498,-19.1567182375816,
8.90339622155706));
#164029=CARTESIAN_POINT('Ctrl Pts',(-16.6273546269492,-19.1611753573282,
8.90366882127507));
#164030=CARTESIAN_POINT('Ctrl Pts',(-16.6281661843242,-19.1691765181999,
8.90415689849131));
#164031=CARTESIAN_POINT('Ctrl Pts',(-16.6285347469306,-19.1727210184805,
8.90437266252171));
#164032=CARTESIAN_POINT('Ctrl Pts',(-16.6293554309751,-19.1804244700756,
8.90484060423676));
#164033=CARTESIAN_POINT('Ctrl Pts',(-16.6298109287508,-19.1845830036479,
8.90509258962364));
#164034=CARTESIAN_POINT('Ctrl Pts',(-16.63112605805,-19.1962695082469,8.90579904903957));
#164035=CARTESIAN_POINT('Ctrl Pts',(-16.632013791217,-19.2037943414982,
8.90625196888426));
#164036=CARTESIAN_POINT('Ctrl Pts',(-16.6375858540321,-19.2489411931032,
8.90895843494798));
#164037=CARTESIAN_POINT('Ctrl Pts',(-16.6432400411717,-19.2864391426249,
8.91116080654894));
#164038=CARTESIAN_POINT('Ctrl Pts',(-16.6652407742255,-19.4097736293278,
8.91831299186595));
#164039=CARTESIAN_POINT('Ctrl Pts',(-16.6858932767267,-19.4947547301422,
8.92309538048254));
#164040=CARTESIAN_POINT('Ctrl Pts',(-16.763495831235,-19.745356798926,8.93736847304226));
#164041=CARTESIAN_POINT('Ctrl Pts',(-16.8357632696252,-19.9054108668867,
8.94677735806602));
#164042=CARTESIAN_POINT('Ctrl Pts',(-16.9388898723586,-20.0744077204743,
8.95828106971673));
#164043=CARTESIAN_POINT('Ctrl Pts',(-16.9512068063274,-20.0938703204419,
8.95963036120592));
#164044=CARTESIAN_POINT('Ctrl Pts',(-16.9690779963049,-20.121115296918,
8.96155590349463));
#164045=CARTESIAN_POINT('Ctrl Pts',(-16.9743714528139,-20.1290673846456,
8.96212242766494));
#164046=CARTESIAN_POINT('Ctrl Pts',(-16.9830590879283,-20.1419287962921,
8.96304618095787));
#164047=CARTESIAN_POINT('Ctrl Pts',(-16.9864205631454,-20.146860129292,
8.96340217173849));
#164048=CARTESIAN_POINT('Ctrl Pts',(-16.9934999693978,-20.1571519409755,
8.96414895452421));
#164049=CARTESIAN_POINT('Ctrl Pts',(-16.9972219110428,-20.1625095727018,
8.96453989679305));
#164050=CARTESIAN_POINT('Ctrl Pts',(-17.0061341818268,-20.1752128234663,
8.96547210932044));
#164051=CARTESIAN_POINT('Ctrl Pts',(-17.0113466462856,-20.1825426917169,
8.96601422503982));
#164052=CARTESIAN_POINT('Ctrl Pts',(-17.0290598810954,-20.2071182701556,
8.96784626185972));
#164053=CARTESIAN_POINT('Ctrl Pts',(-17.0417738558071,-20.2242080435245,
8.96914441020569));
#164054=CARTESIAN_POINT('Ctrl Pts',(-17.0726278652181,-20.2644001943252,
8.97225650732696));
#164055=CARTESIAN_POINT('Ctrl Pts',(-17.0909947202393,-20.2873221174331,
8.97407916674035));
#164056=CARTESIAN_POINT('Ctrl Pts',(-17.2192724498348,-20.4407588338659,
8.98661309298643));
#164057=CARTESIAN_POINT('Ctrl Pts',(-17.344124772451,-20.5579362855098,
8.99793934014697));
#164058=CARTESIAN_POINT('Ctrl Pts',(-17.5621774958484,-20.717926519405,
9.01575850137952));
#164059=CARTESIAN_POINT('Ctrl Pts',(-17.646794521526,-20.7712452944192,
9.0222690312874));
#164060=CARTESIAN_POINT('Ctrl Pts',(-17.7434050317032,-20.8229634804211,
9.02903939677775));
#164061=CARTESIAN_POINT('Ctrl Pts',(-17.7519721099496,-20.827474331368,
9.02963426525452));
#164062=CARTESIAN_POINT('Ctrl Pts',(-17.7646699202641,-20.8340492853774,
9.0305075212119));
#164063=CARTESIAN_POINT('Ctrl Pts',(-17.7687768017727,-20.8361588294532,
9.03078866605437));
#164064=CARTESIAN_POINT('Ctrl Pts',(-17.7760762831955,-20.8398781571396,
9.03128602953067));
#164065=CARTESIAN_POINT('Ctrl Pts',(-17.779266089384,-20.8414933035127,
9.03150258218964));
#164066=CARTESIAN_POINT('Ctrl Pts',(-17.7861106075726,-20.8449372415195,
9.0319655476308));
#164067=CARTESIAN_POINT('Ctrl Pts',(-17.7897665173152,-20.8467635291599,
9.03221180363128));
#164068=CARTESIAN_POINT('Ctrl Pts',(-17.799819868541,-20.8517492968098,
9.03288621613829));
#164069=CARTESIAN_POINT('Ctrl Pts',(-17.8062280981861,-20.8548870723841,
9.03331303726331));
#164070=CARTESIAN_POINT('Ctrl Pts',(-17.8405784776352,-20.8714918850825,
9.03558524960531));
#164071=CARTESIAN_POINT('Ctrl Pts',(-17.868799776498,-20.8843767530646,
9.03739669474941));
#164072=CARTESIAN_POINT('Ctrl Pts',(-18.0476276331995,-20.9613196485517,
9.04859337053058));
#164073=CARTESIAN_POINT('Ctrl Pts',(-18.2049688965256,-21.008358657409,
9.05724256507398));
#164074=CARTESIAN_POINT('Ctrl Pts',(-18.4819453022129,-21.0572262993895,
9.07263611203104));
#164075=CARTESIAN_POINT('Ctrl Pts',(-18.5992018174828,-21.0679710445371,
9.07919659528085));
#164076=CARTESIAN_POINT('Ctrl Pts',(-18.7310339027525,-21.0690462132869,
9.08691992389703));
#164077=CARTESIAN_POINT('Ctrl Pts',(-18.7453331649165,-21.0690179525362,
9.08776197155815));
#164078=CARTESIAN_POINT('Ctrl Pts',(-18.7680875685534,-21.0687424418896,
9.08910925370239));
#164079=CARTESIAN_POINT('Ctrl Pts',(-18.7765435644007,-21.0685893719823,
9.08961154212731));
#164080=CARTESIAN_POINT('Ctrl Pts',(-18.7914537212469,-21.0682300834907,
9.09050013839054));
#164081=CARTESIAN_POINT('Ctrl Pts',(-18.7979083173903,-21.0680449952444,
9.09088577931689));
#164082=CARTESIAN_POINT('Ctrl Pts',(-18.8112551886689,-21.0676011452183,
9.09168525471415));
#164083=CARTESIAN_POINT('Ctrl Pts',(-18.8181472404011,-21.0673382259126,
9.0920992150863));
#164084=CARTESIAN_POINT('Ctrl Pts',(-18.8358317954272,-21.0665770289049,
9.09316436053081));
#164085=CARTESIAN_POINT('Ctrl Pts',(-18.8466218940324,-21.0660298077227,
9.09381707308453));
#164086=CARTESIAN_POINT('Ctrl Pts',(-18.8916136183037,-21.0634026185412,
9.09655077581213));
#164087=CARTESIAN_POINT('Ctrl Pts',(-18.9257648339233,-21.0605751357702,
9.09865504706032));
#164088=CARTESIAN_POINT('Ctrl Pts',(-19.0145326257989,-21.0510514923447,
9.10420412485287));
#164089=CARTESIAN_POINT('Ctrl Pts',(-19.0689807092927,-21.0430530430561,
9.10768722385823));
#164090=CARTESIAN_POINT('Ctrl Pts',(-19.2305112592769,-21.0128533863834,
9.11824910053011));
#164091=CARTESIAN_POINT('Ctrl Pts',(-19.3362455142208,-20.9844706599363,
9.12547629431187));
#164092=CARTESIAN_POINT('Ctrl Pts',(-19.5511457289884,-20.9085356315324,
9.14053240744068));
#164093=CARTESIAN_POINT('Ctrl Pts',(-19.6594797923219,-20.859682499988,
9.14833328767873));
#164094=CARTESIAN_POINT('Ctrl Pts',(-19.7714859151094,-20.7973733340795,
9.15624992791604));
#164095=CARTESIAN_POINT('Ctrl Pts',(-19.7797803067769,-20.7926855581377,
9.15683517993781));
#164096=CARTESIAN_POINT('Ctrl Pts',(-19.7920207576151,-20.7856581237635,
9.15769705759438));
#164097=CARTESIAN_POINT('Ctrl Pts',(-19.7959911808868,-20.7833614528601,
9.15797633999935));
#164098=CARTESIAN_POINT('Ctrl Pts',(-19.8029416813128,-20.7793107668733,
9.15846470105924));
#164099=CARTESIAN_POINT('Ctrl Pts',(-19.8059249533905,-20.7775623384858,
9.15867413608979));
#164100=CARTESIAN_POINT('Ctrl Pts',(-19.8123267211063,-20.7737893036738,
9.15912316835793));
#164101=CARTESIAN_POINT('Ctrl Pts',(-19.8157437961051,-20.7717623868565,
9.15936261225378));
#164102=CARTESIAN_POINT('Ctrl Pts',(-19.8227901980065,-20.7675557901736,
9.15985592728705));
#164103=CARTESIAN_POINT('Ctrl Pts',(-19.8264187367879,-20.7653748169426,
9.16010971397258));
#164104=CARTESIAN_POINT('Ctrl Pts',(-19.8355355022818,-20.7598577892884,
9.16074680186396));
#164105=CARTESIAN_POINT('Ctrl Pts',(-19.8410151779466,-20.7565075913407,
9.16112921779166));
#164106=CARTESIAN_POINT('Ctrl Pts',(-19.856582747576,-20.7468921943585,
9.16221444566273));
#164107=CARTESIAN_POINT('Ctrl Pts',(-19.8666334554969,-20.7405668798271,
9.16291364173717));
#164108=CARTESIAN_POINT('Ctrl Pts',(-19.9002908818686,-20.7189874100909,
9.16525205714589));
#164109=CARTESIAN_POINT('Ctrl Pts',(-19.9236478065596,-20.7033472453639,
9.16686977446889));
#164110=CARTESIAN_POINT('Ctrl Pts',(-20.1082442683675,-20.5743408558051,
9.17967248577959));
#164111=CARTESIAN_POINT('Ctrl Pts',(-20.2532531562015,-20.4394214355165,
9.18992556716932));
#164112=CARTESIAN_POINT('Ctrl Pts',(-20.424216879423,-20.2288501391307,
9.20507586942558));
#164113=CARTESIAN_POINT('Ctrl Pts',(-20.4678646576284,-20.1689186553657,
9.20929909783092));
#164114=CARTESIAN_POINT('Ctrl Pts',(-20.5154192149796,-20.0958557325202,
9.2144143817794));
#164115=CARTESIAN_POINT('Ctrl Pts',(-20.52245796629,-20.0848188061811,9.21518616584822));
#164116=CARTESIAN_POINT('Ctrl Pts',(-20.5337330179475,-20.0667722321823,
9.2164469468045));
#164117=CARTESIAN_POINT('Ctrl Pts',(-20.5380318602532,-20.0598019271727,
9.21693362989756));
#164118=CARTESIAN_POINT('Ctrl Pts',(-20.5456174344879,-20.0473411418383,
9.21780325239325));
#164119=CARTESIAN_POINT('Ctrl Pts',(-20.5489199361723,-20.0418603441908,
9.21818560719888));
#164120=CARTESIAN_POINT('Ctrl Pts',(-20.5558288515399,-20.030275890477,
9.21899350842704));
#164121=CARTESIAN_POINT('Ctrl Pts',(-20.5594295488909,-20.0241689327805,
9.21941925709593));
#164122=CARTESIAN_POINT('Ctrl Pts',(-20.568878182378,-20.0079580215597,
9.22054906880048));
#164123=CARTESIAN_POINT('Ctrl Pts',(-20.5746732706276,-19.997823689589,
9.22125503246142));
#164124=CARTESIAN_POINT('Ctrl Pts',(-20.6012714515754,-19.9504033889682,
9.22455717259818));
#164125=CARTESIAN_POINT('Ctrl Pts',(-20.621026107921,-19.9125436243246,
9.22719045690848));
#164126=CARTESIAN_POINT('Ctrl Pts',(-20.6723571652418,-19.8064639927248,
9.23456546314183));
#164127=CARTESIAN_POINT('Ctrl Pts',(-20.7014639807055,-19.7371246888076,
9.2393846086122));
#164128=CARTESIAN_POINT('Ctrl Pts',(-20.7861203341855,-19.5009724167288,
9.25573273733217));
#164129=CARTESIAN_POINT('Ctrl Pts',(-20.8245915849777,-19.3288216746901,
9.26760507180113));
#164130=CARTESIAN_POINT('Ctrl Pts',(-20.8438467733349,-19.1278429675792,
9.28035989561479));
#164131=CARTESIAN_POINT('Ctrl Pts',(-20.8458598051352,-19.1017413250874,
9.28199389695891));
#164132=CARTESIAN_POINT('Ctrl Pts',(-20.8477953014005,-19.068649097798,
9.28403148483617));
#164133=CARTESIAN_POINT('Ctrl Pts',(-20.8481679332311,-19.0616883834093,
9.28445817244142));
#164134=CARTESIAN_POINT('Ctrl Pts',(-20.8487046762094,-19.0506400795561,
9.28513226954702));
#164135=CARTESIAN_POINT('Ctrl Pts',(-20.8488913281585,-19.0465537075487,
9.28538090892678));
#164136=CARTESIAN_POINT('Ctrl Pts',(-20.8492163337547,-19.0389552462421,
9.28584193904148));
#164137=CARTESIAN_POINT('Ctrl Pts',(-20.8493577838962,-19.0354433924935,
9.28605449553826));
#164138=CARTESIAN_POINT('Ctrl Pts',(-20.84962182659,-19.0284551283484,9.28647643894481));
#164139=CARTESIAN_POINT('Ctrl Pts',(-20.8497445963614,-19.0249787856908,
9.28668583429858));
#164140=CARTESIAN_POINT('Ctrl Pts',(-20.8500062525391,-19.0170131658696,
9.2871645199004));
#164141=CARTESIAN_POINT('Ctrl Pts',(-20.8501394224102,-19.012523700077,
9.28743349581219));
#164142=CARTESIAN_POINT('Ctrl Pts',(-20.8504746950153,-18.9998612810662,
9.28818992515464));
#164143=CARTESIAN_POINT('Ctrl Pts',(-20.8506437464059,-18.9916874338215,
9.28867561948215));
#164144=CARTESIAN_POINT('Ctrl Pts',(-20.8509186141028,-18.9732240514811,
9.28976727070073));
#164145=CARTESIAN_POINT('Ctrl Pts',(-20.8509967709608,-18.9629342724791,
9.29037183225924));
#164146=CARTESIAN_POINT('Ctrl Pts',(-20.8509999019998,-18.9526441527879,
9.29097295163941));
#164147=CARTESIAN_POINT('Ctrl Pts',(-20.8509999014167,-18.952646066426,
9.2909728398501));
#164148=CARTESIAN_POINT('Ctrl Pts',(-20.8510612391861,-18.7516573651538,
9.30271403367758));
#164149=CARTESIAN_POINT('Ctrl Pts',(-20.8225007118581,-18.5516402133368,
9.31315827211277));
#164150=CARTESIAN_POINT('Ctrl Pts',(-20.7530794613129,-18.3138951311856,
9.32683237017865));
#164151=CARTESIAN_POINT('Ctrl Pts',(-20.7385514247039,-18.2696285787851,
9.32943044125517));
#164152=CARTESIAN_POINT('Ctrl Pts',(-20.7225805549386,-18.2258895562519,
9.33206805306779));
#164153=CARTESIAN_POINT('Origin',(-18.734,-18.952,0.));
#164154=CARTESIAN_POINT('',(-20.7225805737622,-18.2258896078036,10.3555828745111));
#164155=CARTESIAN_POINT('',(-20.7225805600179,-18.2258895701625,10.1325349275789));
#164156=CARTESIAN_POINT('',(-20.7225805737622,-18.2258896078036,0.));
#164157=CARTESIAN_POINT('',(-20.8533534905797,-18.9530771009818,10.310943726863));
#164158=CARTESIAN_POINT('Ctrl Pts',(-20.8509997268492,-18.9530754164219,
10.3109437563757));
#164159=CARTESIAN_POINT('Ctrl Pts',(-20.8510361522915,-18.8813704936462,
10.3152783077124));
#164160=CARTESIAN_POINT('Ctrl Pts',(-20.8474252680863,-18.809517619068,
10.319612859049));
#164161=CARTESIAN_POINT('Ctrl Pts',(-20.84014825964,-18.7379240592327,10.3239474103857));
#164162=CARTESIAN_POINT('Ctrl Pts',(-20.8328800282403,-18.6664168508176,
10.328276733673));
#164163=CARTESIAN_POINT('Ctrl Pts',(-20.8219544852784,-18.5951688251049,
10.3326060569603));
#164164=CARTESIAN_POINT('Ctrl Pts',(-20.8074048164118,-18.5245874741187,
10.3369353802477));
#164165=CARTESIAN_POINT('Ctrl Pts',(-20.7928691087987,-18.4540738500436,
10.3412605492975));
#164166=CARTESIAN_POINT('Ctrl Pts',(-20.7747162754983,-18.3842261135468,
10.3455857183473));
#164167=CARTESIAN_POINT('Ctrl Pts',(-20.7530311027464,-18.3154448915115,
10.3499108873972));
#164168=CARTESIAN_POINT('Ctrl Pts',(-20.7435518570418,-18.2853785364498,
10.3518015497685));
#164169=CARTESIAN_POINT('Ctrl Pts',(-20.7333983034435,-18.2555158565498,
10.3536922121398));
#164170=CARTESIAN_POINT('Ctrl Pts',(-20.7225805737622,-18.2258896078036,
10.3555828745111));
#164171=CARTESIAN_POINT('Ctrl Pts',(-20.7242503992901,-18.225264130614,
9.55561792115202));
#164172=CARTESIAN_POINT('Ctrl Pts',(-20.5136266149504,-17.6645819491398,
9.59172753140163));
#164173=CARTESIAN_POINT('Ctrl Pts',(-19.5197098403558,-16.6327270633957,
9.67022907721175));
#164174=CARTESIAN_POINT('Ctrl Pts',(-17.2597753314279,-16.928885683341,
9.7911225585823));
#164175=CARTESIAN_POINT('Ctrl Pts',(-16.234911172256,-19.0965162369475,
9.91829836526374));
#164176=CARTESIAN_POINT('Ctrl Pts',(-17.5028059015931,-21.1315621128439,
10.0454741719452));
#164177=CARTESIAN_POINT('Ctrl Pts',(-19.9002447996946,-21.1669950290873,
10.1726499786266));
#164178=CARTESIAN_POINT('Ctrl Pts',(-20.823916190907,-19.7776853379838,
10.2611398283041));
#164179=CARTESIAN_POINT('Ctrl Pts',(-20.8542039878978,-19.0144660717243,
10.307237742421));
#164180=CARTESIAN_POINT('Ctrl Pts',(-20.8538228835136,-18.9530774369206,
10.3109437209775));
#164181=CARTESIAN_POINT('Ctrl Pts',(-20.7225805549386,-18.2258895562519,
9.33206805306779));
#164182=CARTESIAN_POINT('Ctrl Pts',(-20.7083722868681,-18.1869777270011,
9.33441456870847));
#164183=CARTESIAN_POINT('Ctrl Pts',(-20.693022084485,-18.1484834091484,
9.33679231958261));
#164184=CARTESIAN_POINT('Ctrl Pts',(-20.6684009409741,-18.0916500373935,
9.34040228155194));
#164185=CARTESIAN_POINT('Ctrl Pts',(-20.6599812432231,-18.0729634445399,
9.34160564671993));
#164186=CARTESIAN_POINT('Ctrl Pts',(-20.6475367865955,-18.0463817588176,
9.34334232161629));
#164187=CARTESIAN_POINT('Ctrl Pts',(-20.6437315490788,-18.0383847422257,
9.34386805941979));
#164188=CARTESIAN_POINT('Ctrl Pts',(-20.6370470760901,-18.0245610188386,
9.34478263147945));
#164189=CARTESIAN_POINT('Ctrl Pts',(-20.6341909604698,-18.018723219035,
9.34517065749221));
#164190=CARTESIAN_POINT('Ctrl Pts',(-20.6286470865644,-18.0075226843942,
9.34591864013509));
#164191=CARTESIAN_POINT('Ctrl Pts',(-20.6259633240403,-18.0021580333254,
9.34627845405013));
#164192=CARTESIAN_POINT('Ctrl Pts',(-20.6188715792595,-17.9881314462617,
9.34722336186107));
#164193=CARTESIAN_POINT('Ctrl Pts',(-20.6144267212519,-17.9794884061054,
9.34780974861588));
#164194=CARTESIAN_POINT('Ctrl Pts',(-20.5987863527489,-17.9495837948224,
9.34985325187573));
#164195=CARTESIAN_POINT('Ctrl Pts',(-20.5872888088139,-17.9284830698622,
9.35132101656207));
#164196=CARTESIAN_POINT('Ctrl Pts',(-20.5034337443168,-17.7806362921786,
9.36179370081421));
#164197=CARTESIAN_POINT('Ctrl Pts',(-20.4185109288099,-17.661497100169,
9.37126612649183));
#164198=CARTESIAN_POINT('Ctrl Pts',(-20.2315225656315,-17.4493862964996,
9.38992778565965));
#164199=CARTESIAN_POINT('Ctrl Pts',(-20.1312641286651,-17.355729239754,
9.39904487547204));
#164200=CARTESIAN_POINT('Ctrl Pts',(-20.0125804274804,-17.2646700196703,
9.40841273773673));
#164201=CARTESIAN_POINT('Ctrl Pts',(-20.0024322036148,-17.2570279843549,
9.40920319335917));
#164202=CARTESIAN_POINT('Ctrl Pts',(-19.986797717762,-17.2454736267136,
9.41040415758955));
#164203=CARTESIAN_POINT('Ctrl Pts',(-19.9813607286224,-17.2414955130815,
9.41081872957315));
#164204=CARTESIAN_POINT('Ctrl Pts',(-19.9723708049154,-17.2349834620866,
9.41149904499264));
#164205=CARTESIAN_POINT('Ctrl Pts',(-19.9688289060965,-17.2324344690082,
9.4117657678084));
#164206=CARTESIAN_POINT('Ctrl Pts',(-19.9619672187143,-17.2275284619199,
9.41227991712364));
#164207=CARTESIAN_POINT('Ctrl Pts',(-19.9586484656496,-17.2251700396066,
9.4125274378999));
#164208=CARTESIAN_POINT('Ctrl Pts',(-19.9553132035222,-17.2228143364453,
9.4127750168183));
#164209=CARTESIAN_POINT('Ctrl Pts',(-19.9553035097842,-17.2228074898584,
9.41277573638156));
#164210=CARTESIAN_POINT('Ctrl Pts',(-19.9552840880669,-17.2227937727453,
9.41277717802993));
#164211=CARTESIAN_POINT('Ctrl Pts',(-19.9552743598493,-17.2227869020515,
9.41277790013266));
#164212=CARTESIAN_POINT('Ctrl Pts',(-19.9552548689621,-17.2227731365783,
9.41277934687539));
#164213=CARTESIAN_POINT('Ctrl Pts',(-19.9552451061013,-17.2227662416647,
9.41278007152951));
#164214=CARTESIAN_POINT('Ctrl Pts',(-19.9552249124328,-17.2227519803636,
9.4127815703957));
#164215=CARTESIAN_POINT('Ctrl Pts',(-19.9552144819454,-17.2227446142198,
9.41278234458257));
#164216=CARTESIAN_POINT('Ctrl Pts',(-19.9551934527626,-17.2227297634267,
9.41278390541815));
#164217=CARTESIAN_POINT('Ctrl Pts',(-19.9551828540166,-17.2227222787464,
9.41278469207022));
#164218=CARTESIAN_POINT('Ctrl Pts',(-19.9551614847679,-17.2227071883879,
9.41278627809847));
#164219=CARTESIAN_POINT('Ctrl Pts',(-19.955150714365,-17.2226995827851,
9.41278707746685));
#164220=CARTESIAN_POINT('Ctrl Pts',(-19.9551289980691,-17.2226842479598,
9.4127886892036));
#164221=CARTESIAN_POINT('Ctrl Pts',(-19.9551180522886,-17.2226765188218,
9.41278950156323));
#164222=CARTESIAN_POINT('Ctrl Pts',(-19.9550959819521,-17.222660934621,
9.41279113952513));
#164223=CARTESIAN_POINT('Ctrl Pts',(-19.9550848567631,-17.2226530791165,
9.41279196517394));
#164224=CARTESIAN_POINT('Ctrl Pts',(-19.9550624232963,-17.2226372391527,
9.41279363003305));
#164225=CARTESIAN_POINT('Ctrl Pts',(-19.9550511154003,-17.2226292549683,
9.41279446921457));
#164226=CARTESIAN_POINT('Ctrl Pts',(-19.9550283126131,-17.2226131549028,
9.41279616142769));
#164227=CARTESIAN_POINT('Ctrl Pts',(-19.9550168174606,-17.2226050388427,
9.41279701447822));
#164228=CARTESIAN_POINT('Ctrl Pts',(-19.9549936360609,-17.2225886721478,
9.41279873473222));
#164229=CARTESIAN_POINT('Ctrl Pts',(-19.954981949856,-17.2225804215488,
9.41279960193207));
#164230=CARTESIAN_POINT('Ctrl Pts',(-19.9549583818049,-17.2225637825835,
9.41280135082069));
#164231=CARTESIAN_POINT('Ctrl Pts',(-19.9549465003227,-17.2225553944803,
9.41280223248196));
#164232=CARTESIAN_POINT('Ctrl Pts',(-19.9549225375747,-17.2225384776004,
9.41280401059931));
#164233=CARTESIAN_POINT('Ctrl Pts',(-19.9549104561934,-17.2225299487484,
9.41280490706346));
#164234=CARTESIAN_POINT('Ctrl Pts',(-19.9548860894242,-17.2225127474085,
9.41280671509841));
#164235=CARTESIAN_POINT('Ctrl Pts',(-19.9548738037708,-17.2225040747396,
9.41280762668838));
#164236=CARTESIAN_POINT('Ctrl Pts',(-19.954849023501,-17.2224865822866,
9.41280946534114));
#164237=CARTESIAN_POINT('Ctrl Pts',(-19.9548365292056,-17.2224777627359,
9.41281039237957));
#164238=CARTESIAN_POINT('Ctrl Pts',(-19.9548113270583,-17.2224599732969,
9.41281226226843));
#164239=CARTESIAN_POINT('Ctrl Pts',(-19.9547986189937,-17.2224510032656,
9.41281320513407));
#164240=CARTESIAN_POINT('Ctrl Pts',(-19.9547729843128,-17.2224329093608,
9.41281510704624));
#164241=CARTESIAN_POINT('Ctrl Pts',(-19.9547600578991,-17.2224237856375,
9.41281606607716));
#164242=CARTESIAN_POINT('Ctrl Pts',(-19.9547339816052,-17.2224053809018,
9.41281800068272));
#164243=CARTESIAN_POINT('Ctrl Pts',(-19.9547208315242,-17.2223960997552,
9.41281897627167));
#164244=CARTESIAN_POINT('Ctrl Pts',(-19.951870266171,-17.2203842585756,
9.41303045238298));
#164245=CARTESIAN_POINT('Ctrl Pts',(-19.9490279680683,-17.2183887119179,
9.41324046161644));
#164246=CARTESIAN_POINT('Ctrl Pts',(-19.9424087532231,-17.2137657082699,
9.41372757341653));
#164247=CARTESIAN_POINT('Ctrl Pts',(-19.938628177307,-17.2111435661814,
9.41400431194887));
#164248=CARTESIAN_POINT('Ctrl Pts',(-19.9269336109555,-17.2030887548029,
9.4148559093759));
#164249=CARTESIAN_POINT('Ctrl Pts',(-19.9189910687996,-17.1976974837754,
9.41542802846367));
#164250=CARTESIAN_POINT('Ctrl Pts',(-19.8165021452211,-17.1291432850232,
9.4227343206875));
#164251=CARTESIAN_POINT('Ctrl Pts',(-19.7170385839675,-17.0736336969328,
9.42900129176324));
#164252=CARTESIAN_POINT('Ctrl Pts',(-19.5099110081263,-16.9790220714055,
9.44141172097439));
#164253=CARTESIAN_POINT('Ctrl Pts',(-19.4025859821442,-16.9401173508394,
9.44753902465469));
#164254=CARTESIAN_POINT('Ctrl Pts',(-19.2395033464369,-16.8955001555529,
9.45694031242375));
#164255=CARTESIAN_POINT('Ctrl Pts',(-19.1858102281003,-16.883040813327,
9.46004739935269));
#164256=CARTESIAN_POINT('Ctrl Pts',(-19.0980015787013,-16.8662462709348,
9.46519076290448));
#164257=CARTESIAN_POINT('Ctrl Pts',(-19.0641581411941,-16.8606221831351,
9.46718766487111));
#164258=CARTESIAN_POINT('Ctrl Pts',(-19.0194921615275,-16.854310783408,
9.46984807196404));
#164259=CARTESIAN_POINT('Ctrl Pts',(-19.0087787034061,-16.8528805462059,
9.47048805418126));
#164260=CARTESIAN_POINT('Ctrl Pts',(-18.9912106967492,-16.8506720291598,
9.47154073141431));
#164261=CARTESIAN_POINT('Ctrl Pts',(-18.9843623816266,-16.849845091414,
9.47195188531553));
#164262=CARTESIAN_POINT('Ctrl Pts',(-18.971096197473,-16.8483089380086,
9.47274995070855));
#164263=CARTESIAN_POINT('Ctrl Pts',(-18.9646788776244,-16.8475955842225,
9.47313672686161));
#164264=CARTESIAN_POINT('Ctrl Pts',(-18.9498510739405,-16.846015954469,
9.47403212231116));
#164265=CARTESIAN_POINT('Ctrl Pts',(-18.9414385054595,-16.8451706881274,
9.47454139781465));
#164266=CARTESIAN_POINT('Ctrl Pts',(-18.9187937471432,-16.8430323624584,
9.47591577269443));
#164267=CARTESIAN_POINT('Ctrl Pts',(-18.9045533446997,-16.8418330004304,
9.47678380057848));
#164268=CARTESIAN_POINT('Ctrl Pts',(-18.7737124648666,-16.8321463301725,
9.48479481068193));
#164269=CARTESIAN_POINT('Ctrl Pts',(-18.6566273911351,-16.8331884646397,
9.49223989754308));
#164270=CARTESIAN_POINT('Ctrl Pts',(-18.3780211176261,-16.8587952442312,
9.51051541238347));
#164271=CARTESIAN_POINT('Ctrl Pts',(-18.2180669964656,-16.892378590209,
9.52148636061821));
#164272=CARTESIAN_POINT('Ctrl Pts',(-18.0329154722312,-16.9541981160818,
9.53388725072007));
#164273=CARTESIAN_POINT('Ctrl Pts',(-18.0025201118048,-16.9651257414575,
9.53591097297362));
#164274=CARTESIAN_POINT('Ctrl Pts',(-17.9656436836677,-16.9793444875725,
9.53834125681395));
#164275=CARTESIAN_POINT('Ctrl Pts',(-17.9589157453101,-16.9819782739377,
9.53878362011833));
#164276=CARTESIAN_POINT('Ctrl Pts',(-17.9483851474728,-16.9861629858148,
9.53947423925572));
#164277=CARTESIAN_POINT('Ctrl Pts',(-17.9445733661544,-16.9876905912537,
9.53972385876421));
#164278=CARTESIAN_POINT('Ctrl Pts',(-17.9374539198243,-16.9905678436766,
9.54018936826387));
#164279=CARTESIAN_POINT('Ctrl Pts',(-17.9341452627771,-16.9919147566312,
9.54040541251055));
#164280=CARTESIAN_POINT('Ctrl Pts',(-17.9265966060468,-16.9950100171784,
9.54089765860845));
#164281=CARTESIAN_POINT('Ctrl Pts',(-17.9223588764044,-16.9967637685364,
9.54117352963987));
#164282=CARTESIAN_POINT('Ctrl Pts',(-17.9093381867666,-17.0022019059693,
9.5420198104028));
#164283=CARTESIAN_POINT('Ctrl Pts',(-17.900574225172,-17.0059318616222,
9.54258752958714));
#164284=CARTESIAN_POINT('Ctrl Pts',(-17.7829225667688,-17.0569451505327,
9.55018714534813));
#164285=CARTESIAN_POINT('Ctrl Pts',(-17.6781579354447,-17.113253995431,
9.55670911330969));
#164286=CARTESIAN_POINT('Ctrl Pts',(-17.4871063525511,-17.2376833368706,
9.56912161114755));
#164287=CARTESIAN_POINT('Ctrl Pts',(-17.4003110645262,-17.304305150168,
9.57500500383094));
#164288=CARTESIAN_POINT('Ctrl Pts',(-17.2781424346921,-17.4140818850209,
9.58413842023623));
#164289=CARTESIAN_POINT('Ctrl Pts',(-17.2386866174734,-17.4524165161774,
9.58723967848758));
#164290=CARTESIAN_POINT('Ctrl Pts',(-17.1771493661918,-17.5170510364593,
9.59237425294312));
#164291=CARTESIAN_POINT('Ctrl Pts',(-17.1541356542176,-17.5424288321776,
9.59436837072523));
#164292=CARTESIAN_POINT('Ctrl Pts',(-17.1246880112075,-17.5765289442296,
9.59702559403794));
#164293=CARTESIAN_POINT('Ctrl Pts',(-17.1176901501293,-17.5847589220637,
9.59766524846115));
#164294=CARTESIAN_POINT('Ctrl Pts',(-17.1063284108698,-17.5983302601747,
9.59871752386693));
#164295=CARTESIAN_POINT('Ctrl Pts',(-17.1019270493646,-17.6036400893478,
9.59912860604435));
#164296=CARTESIAN_POINT('Ctrl Pts',(-17.0934551872237,-17.6139628499704,
9.59992663043414));
#164297=CARTESIAN_POINT('Ctrl Pts',(-17.0893815171522,-17.6189730902832,
9.60031343782762));
#164298=CARTESIAN_POINT('Ctrl Pts',(-17.0800251602083,-17.6305887215608,
9.60120904874766));
#164299=CARTESIAN_POINT('Ctrl Pts',(-17.0747590356788,-17.6372072571977,
9.60171850947502));
#164300=CARTESIAN_POINT('Ctrl Pts',(-17.060695731012,-17.6551012576845,
9.60309370839287));
#164301=CARTESIAN_POINT('Ctrl Pts',(-17.0519730297208,-17.6664344513281,
9.60396238055695));
#164302=CARTESIAN_POINT('Ctrl Pts',(-16.9725011987249,-17.7718838106393,
9.61202503360709));
#164303=CARTESIAN_POINT('Ctrl Pts',(-16.9096159195966,-17.8716449675874,
9.6195256589858));
#164304=CARTESIAN_POINT('Ctrl Pts',(-16.7799641013343,-18.1212299050466,
9.63790280092094));
#164305=CARTESIAN_POINT('Ctrl Pts',(-16.7216460278061,-18.2746026979024,
9.64891778688076));
#164306=CARTESIAN_POINT('Ctrl Pts',(-16.673972600071,-18.4631896181054,
9.66125994868755));
#164307=CARTESIAN_POINT('Ctrl Pts',(-16.667040583935,-18.4933852546187,
9.6631992582693));
#164308=CARTESIAN_POINT('Ctrl Pts',(-16.6593305632245,-18.530708422663,
9.66554227879331));
#164309=CARTESIAN_POINT('Ctrl Pts',(-16.657923022374,-18.5377002880341,
9.66597888455284));
#164310=CARTESIAN_POINT('Ctrl Pts',(-16.6557647001057,-18.5487088727017,
9.66666252450698));
#164311=CARTESIAN_POINT('Ctrl Pts',(-16.6549901826835,-18.5527208054027,
9.66691087816413));
#164312=CARTESIAN_POINT('Ctrl Pts',(-16.6535596877785,-18.5602476652057,
9.66737530614509));
#164313=CARTESIAN_POINT('Ctrl Pts',(-16.652901007267,-18.5637619709658,
9.66759152706062));
#164314=CARTESIAN_POINT('Ctrl Pts',(-16.6514119893932,-18.5718191166709,
9.66808584549477));
#164315=CARTESIAN_POINT('Ctrl Pts',(-16.6505876122524,-18.5763630083733,
9.66836360151432));
#164316=CARTESIAN_POINT('Ctrl Pts',(-16.6480800127015,-18.5904468920974,
9.66922145916228));
#164317=CARTESIAN_POINT('Ctrl Pts',(-16.6464473706886,-18.5999959216786,
9.66979876239972));
#164318=CARTESIAN_POINT('Ctrl Pts',(-16.6280527697977,-18.7122143456564,
9.67653585815283));
#164319=CARTESIAN_POINT('Ctrl Pts',(-16.6188126508804,-18.8159881285185,
9.68230549738156));
#164320=CARTESIAN_POINT('Ctrl Pts',(-16.6155502458532,-19.0320130549256,
9.69411211035283));
#164321=CARTESIAN_POINT('Ctrl Pts',(-16.6227475512994,-19.1439489123726,
9.70012213012779));
#164322=CARTESIAN_POINT('Ctrl Pts',(-16.6477177264939,-19.3167366506037,
9.70977486139479));
#164323=CARTESIAN_POINT('Ctrl Pts',(-16.6594120857905,-19.3782518614796,
9.71328513596411));
#164324=CARTESIAN_POINT('Ctrl Pts',(-16.6824641905068,-19.4757394758118,
9.71903241786779));
#164325=CARTESIAN_POINT('Ctrl Pts',(-16.6920873804407,-19.512084648973,
9.72121677335223));
#164326=CARTESIAN_POINT('Ctrl Pts',(-16.7058182040965,-19.5588709717385,
9.72409087483164));
#164327=CARTESIAN_POINT('Ctrl Pts',(-16.709048499029,-19.5695639117193,
9.72475200050965));
#164328=CARTESIAN_POINT('Ctrl Pts',(-16.7144339173746,-19.5868941073688,
9.725830621063));
#164329=CARTESIAN_POINT('Ctrl Pts',(-16.716537527734,-19.5935472397802,
9.72624642314144));
#164330=CARTESIAN_POINT('Ctrl Pts',(-16.7206422381173,-19.6063094427599,
9.72704737572249));
#164331=CARTESIAN_POINT('Ctrl Pts',(-16.7226383501965,-19.6124200455045,
9.72743235816625));
#164332=CARTESIAN_POINT('Ctrl Pts',(-16.7272668326533,-19.6263733625366,
9.72831488785078));
#164333=CARTESIAN_POINT('Ctrl Pts',(-16.7299173925248,-19.634209891756,
9.72881303188787));
#164334=CARTESIAN_POINT('Ctrl Pts',(-16.7370684358692,-19.6549510003284,
9.7301381978387));
#164335=CARTESIAN_POINT('Ctrl Pts',(-16.7416480114709,-19.6678277172201,
9.73096783087606));
#164336=CARTESIAN_POINT('Ctrl Pts',(-16.7766618073855,-19.7633389375787,
9.73717419648778));
#164337=CARTESIAN_POINT('Ctrl Pts',(-16.812097029624,-19.8440365347385,
9.74271836954522));
#164338=CARTESIAN_POINT('Ctrl Pts',(-16.9364588089905,-20.0851954432848,
9.76021705858079));
#164339=CARTESIAN_POINT('Ctrl Pts',(-17.0412592928378,-20.2364869505178,
9.77261274122918));
#164340=CARTESIAN_POINT('Ctrl Pts',(-17.191737782315,-20.4027921293093,
9.78696996107506));
#164341=CARTESIAN_POINT('Ctrl Pts',(-17.2201307774278,-20.4323955688644,
9.7895547854379));
#164342=CARTESIAN_POINT('Ctrl Pts',(-17.2548888246814,-20.4665887591102,
9.79255618039699));
#164343=CARTESIAN_POINT('Ctrl Pts',(-17.2604395906209,-20.471989704681,
9.79303074643446));
#164344=CARTESIAN_POINT('Ctrl Pts',(-17.2690603341368,-20.4802861579751,
9.79376030383381));
#164345=CARTESIAN_POINT('Ctrl Pts',(-17.2721094725527,-20.4832030863847,
9.79401691737003));
#164346=CARTESIAN_POINT('Ctrl Pts',(-17.2777479272629,-20.4885648642243,
9.79448878269691));
#164347=CARTESIAN_POINT('Ctrl Pts',(-17.2803346721282,-20.491012279418,
9.79470423015101));
#164348=CARTESIAN_POINT('Ctrl Pts',(-17.2861556263775,-20.4964919305224,
9.79518675590144));
#164349=CARTESIAN_POINT('Ctrl Pts',(-17.2893931816891,-20.4995205313635,
9.79545355501102));
#164350=CARTESIAN_POINT('Ctrl Pts',(-17.2976821399734,-20.5072258331796,
9.79613268854724));
#164351=CARTESIAN_POINT('Ctrl Pts',(-17.3027469278445,-20.5118881477864,
9.79654394849598));
#164352=CARTESIAN_POINT('Ctrl Pts',(-17.3321057823056,-20.5386506264751,
9.79890719523391));
#164353=CARTESIAN_POINT('Ctrl Pts',(-17.3568902072886,-20.5602090953013,
9.80082100703645));
#164354=CARTESIAN_POINT('Ctrl Pts',(-17.3964519373815,-20.5930358616361,
9.80376971246546));
#164355=CARTESIAN_POINT('Ctrl Pts',(-17.4108917784791,-20.6047002723072,
9.80482473092535));
#164356=CARTESIAN_POINT('Ctrl Pts',(-17.4266454598076,-20.6170871721849,
9.80595529142207));
#164357=CARTESIAN_POINT('Ctrl Pts',(-17.4278083413471,-20.6179995605097,
9.80603862655496));
#164358=CARTESIAN_POINT('Ctrl Pts',(-17.4470160553447,-20.6330373190721,
9.80741315832312));
#164359=CARTESIAN_POINT('Ctrl Pts',(-17.4652885787107,-20.6468703561365,
9.80869249735971));
#164360=CARTESIAN_POINT('Ctrl Pts',(-17.5206414204066,-20.6873777984211,
9.81249581259531));
#164361=CARTESIAN_POINT('Ctrl Pts',(-17.55836466111,-20.7131521604237,9.81499332195534));
#164362=CARTESIAN_POINT('Ctrl Pts',(-17.6891295565142,-20.796421901009,
9.82343362746429));
#164363=CARTESIAN_POINT('Ctrl Pts',(-17.7857773243761,-20.8479217458387,
9.82932172188505));
#164364=CARTESIAN_POINT('Ctrl Pts',(-17.93646187295,-20.9137999556882,9.83846606798689));
#164365=CARTESIAN_POINT('Ctrl Pts',(-17.9877968341766,-20.9338946289288,
9.84157359006515));
#164366=CARTESIAN_POINT('Ctrl Pts',(-18.0722657369381,-20.9632120182653,
9.84671760971191));
#164367=CARTESIAN_POINT('Ctrl Pts',(-18.1049439369301,-20.9736711627375,
9.84871471944941));
#164368=CARTESIAN_POINT('Ctrl Pts',(-18.148232057548,-20.9863750269638,
9.85137536412097));
#164369=CARTESIAN_POINT('Ctrl Pts',(-18.1586265816501,-20.9893392588462,
9.85201537078315));
#164370=CARTESIAN_POINT('Ctrl Pts',(-18.1756912088485,-20.9940646117463,
9.85306807798253));
#164371=CARTESIAN_POINT('Ctrl Pts',(-18.1823481078044,-20.9958729835606,
9.85347923723297));
#164372=CARTESIAN_POINT('Ctrl Pts',(-18.1952528776695,-20.9993109751234,
9.85427730568879));
#164373=CARTESIAN_POINT('Ctrl Pts',(-18.2014996065773,-21.0009446113187,
9.85466407951666));
#164374=CARTESIAN_POINT('Ctrl Pts',(-18.2159429958744,-21.0046513154476,
9.8555594589186));
#164375=CARTESIAN_POINT('Ctrl Pts',(-18.2241447559066,-21.0067038981721,
9.85606872062577));
#164376=CARTESIAN_POINT('Ctrl Pts',(-18.246241475799,-21.0120934020021,
9.85744303413447));
#164377=CARTESIAN_POINT('Ctrl Pts',(-18.260158105327,-21.0153388102875,
9.85831101403678));
#164378=CARTESIAN_POINT('Ctrl Pts',(-18.3881654428184,-21.0438272672115,
9.86631836257877));
#164379=CARTESIAN_POINT('Ctrl Pts',(-18.5041115851046,-21.0597206566284,
9.87375951567205));
#164380=CARTESIAN_POINT('Ctrl Pts',(-18.7832505341023,-21.0746733398998,
9.89201886651903));
#164381=CARTESIAN_POINT('Ctrl Pts',(-18.9461977362871,-21.0646144742368,
9.90297711948184));
#164382=CARTESIAN_POINT('Ctrl Pts',(-19.13838591786,-21.0302728115179,9.91538262553902));
#164383=CARTESIAN_POINT('Ctrl Pts',(-19.1702543746321,-21.023817617185,
9.91742016143153));
#164384=CARTESIAN_POINT('Ctrl Pts',(-19.2090240487272,-21.0150301904209,
9.91986468832512));
#164385=CARTESIAN_POINT('Ctrl Pts',(-19.2160765319396,-21.0133936145963,
9.9203079676584));
#164386=CARTESIAN_POINT('Ctrl Pts',(-19.227119094561,-21.0107713443097,
9.92099969674291));
#164387=CARTESIAN_POINT('Ctrl Pts',(-19.2311148580123,-21.0098101730185,
9.92124951725988));
#164388=CARTESIAN_POINT('Ctrl Pts',(-19.2385782094178,-21.0079918747214,
9.92171520067195));
#164389=CARTESIAN_POINT('Ctrl Pts',(-19.2420463889075,-21.0071376171167,
9.92193121903391));
#164390=CARTESIAN_POINT('Ctrl Pts',(-19.2499580327486,-21.0051676251089,
9.92242314597205));
#164391=CARTESIAN_POINT('Ctrl Pts',(-19.2544000391822,-21.0040462442347,
9.92269872538134));
#164392=CARTESIAN_POINT('Ctrl Pts',(-19.2680411717368,-21.0005554089983,
9.92354322312421));
#164393=CARTESIAN_POINT('Ctrl Pts',(-19.2772281640435,-20.9981384132661,
9.92410946732902));
#164394=CARTESIAN_POINT('Ctrl Pts',(-19.359553736834,-20.9758859085876,
9.92916366286775));
#164395=CARTESIAN_POINT('Ctrl Pts',(-19.4316028334109,-20.9521961229144,
9.93344583061162));
#164396=CARTESIAN_POINT('Ctrl Pts',(-19.542054282036,-20.909182534394,9.9400066127025));
#164397=CARTESIAN_POINT('Ctrl Pts',(-19.5813975995392,-20.8924722853381,
9.94234267543521));
#164398=CARTESIAN_POINT('Ctrl Pts',(-19.7194907212765,-20.8288186372802,
9.95062118388836));
#164399=CARTESIAN_POINT('Ctrl Pts',(-19.8150774026979,-20.7754338269768,
9.9565078831916));
#164400=CARTESIAN_POINT('Ctrl Pts',(-19.9519739514086,-20.6844150185626,
9.96564898592232));
#164401=CARTESIAN_POINT('Ctrl Pts',(-19.9966274788677,-20.6521451550111,
9.96875464900143));
#164402=CARTESIAN_POINT('Ctrl Pts',(-20.0669593893852,-20.5970179989424,
9.97389586568113));
#164403=CARTESIAN_POINT('Ctrl Pts',(-20.0934296045401,-20.5752116019047,
9.97589208771736));
#164404=CARTESIAN_POINT('Ctrl Pts',(-20.1275293215633,-20.5457006695304,
9.97855171732225));
#164405=CARTESIAN_POINT('Ctrl Pts',(-20.1356467600953,-20.5385661497325,
9.97919161952712));
#164406=CARTESIAN_POINT('Ctrl Pts',(-20.1488551361408,-20.5267766581802,
9.98024419867555));
#164407=CARTESIAN_POINT('Ctrl Pts',(-20.1539786414091,-20.5221583473088,
9.98065533506835));
#164408=CARTESIAN_POINT('Ctrl Pts',(-20.1638543634474,-20.5131685341615,
9.98145339044124));
#164409=CARTESIAN_POINT('Ctrl Pts',(-20.1686093357178,-20.5088001622443,
9.98184017420952));
#164410=CARTESIAN_POINT('Ctrl Pts',(-20.1795448204575,-20.4986611363548,
9.98273562220575));
#164411=CARTESIAN_POINT('Ctrl Pts',(-20.185710861493,-20.4928750987813,
9.983244942883));
#164412=CARTESIAN_POINT('Ctrl Pts',(-20.2022061746189,-20.4772094698592,
9.98461951871922));
#164413=CARTESIAN_POINT('Ctrl Pts',(-20.2124701892517,-20.4672620835693,
9.98548770371838));
#164414=CARTESIAN_POINT('Ctrl Pts',(-20.3058954028151,-20.374865905961,
9.993510868046));
#164415=CARTESIAN_POINT('Ctrl Pts',(-20.3821685934173,-20.2857672119175,
10.0009690164536));
#164416=CARTESIAN_POINT('Ctrl Pts',(-20.5463777589345,-20.0582193214209,
10.0193001074059));
#164417=CARTESIAN_POINT('Ctrl Pts',(-20.6263877603084,-19.9149657795901,
10.0303152447319));
#164418=CARTESIAN_POINT('Ctrl Pts',(-20.7012121944736,-19.7347904123535,
10.0427007793794));
#164419=CARTESIAN_POINT('Ctrl Pts',(-20.7126617703775,-19.7053807093284,
10.0446771132839));
#164420=CARTESIAN_POINT('Ctrl Pts',(-20.7259025060463,-19.6689831676142,
10.0470584570095));
#164421=CARTESIAN_POINT('Ctrl Pts',(-20.7283205551941,-19.6622295282239,
10.0474976225049));
#164422=CARTESIAN_POINT('Ctrl Pts',(-20.7320650322533,-19.6516012410794,
10.0481843659083));
#164423=CARTESIAN_POINT('Ctrl Pts',(-20.7334145990411,-19.6477348858806,
10.0484332828604));
#164424=CARTESIAN_POINT('Ctrl Pts',(-20.7359210084457,-19.640486782705,
10.0488981891431));
#164425=CARTESIAN_POINT('Ctrl Pts',(-20.7370804929386,-19.637106059703,
10.0491143284831));
#164426=CARTESIAN_POINT('Ctrl Pts',(-20.7397139282448,-19.6293638844503,
10.0496077112137));
#164427=CARTESIAN_POINT('Ctrl Pts',(-20.7411822149267,-19.6250005578846,
10.049884617916));
#164428=CARTESIAN_POINT('Ctrl Pts',(-20.7456726550282,-19.6115108429495,
10.0507372482103));
#164429=CARTESIAN_POINT('Ctrl Pts',(-20.748646933026,-19.6023684848468,
10.0513102223729));
#164430=CARTESIAN_POINT('Ctrl Pts',(-20.7774525867324,-19.5117313046548,
10.0569454585948));
#164431=CARTESIAN_POINT('Ctrl Pts',(-20.7983905120187,-19.4287525255262,
10.0617451793867));
#164432=CARTESIAN_POINT('Ctrl Pts',(-20.8385991730742,-19.215768687721,
10.0736795592272));
#164433=CARTESIAN_POINT('Ctrl Pts',(-20.8509009167197,-19.084827760392,
10.080678612438));
#164434=CARTESIAN_POINT('Ctrl Pts',(-20.8510686213948,-18.8613529327797,
10.093037908689));
#164435=CARTESIAN_POINT('Ctrl Pts',(-20.8451100147201,-18.7692216670311,
10.098249111993));
#164436=CARTESIAN_POINT('Ctrl Pts',(-20.8313804902798,-18.6641219290087,
10.1044627695678));
#164437=CARTESIAN_POINT('Ctrl Pts',(-20.8294631848653,-18.650482616976,
10.1052742662429));
#164438=CARTESIAN_POINT('Ctrl Pts',(-20.8261768230356,-18.6286517394469,
10.1065817451484));
#164439=CARTESIAN_POINT('Ctrl Pts',(-20.8248923983709,-18.6204476935897,
10.1070750504501));
#164440=CARTESIAN_POINT('Ctrl Pts',(-20.8225273356136,-18.6059018162024,
10.107953241767));
#164441=CARTESIAN_POINT('Ctrl Pts',(-20.8214659899547,-18.5995569211838,
10.108337511021));
#164442=CARTESIAN_POINT('Ctrl Pts',(-20.8191956396225,-18.5863545005389,
10.1091396443378));
#164443=CARTESIAN_POINT('Ctrl Pts',(-20.8179816892408,-18.5794979142568,
10.1095576615708));
#164444=CARTESIAN_POINT('Ctrl Pts',(-20.8147441180365,-18.561722890938,
10.1106451137707));
#164445=CARTESIAN_POINT('Ctrl Pts',(-20.812668397939,-18.5508142691322,
10.111316201506));
#164446=CARTESIAN_POINT('Ctrl Pts',(-20.8033102379476,-18.5036573840885,
10.1142336751931));
#164447=CARTESIAN_POINT('Ctrl Pts',(-20.7951650834556,-18.4675888208255,
10.1165074352853));
#164448=CARTESIAN_POINT('Ctrl Pts',(-20.7710540903731,-18.3724844626009,
10.1226194797501));
#164449=CARTESIAN_POINT('Ctrl Pts',(-20.7534686062404,-18.3138988507035,
10.1265064549792));
#164450=CARTESIAN_POINT('Ctrl Pts',(-20.7298520795935,-18.2460408765856,
10.131146311054));
#164451=CARTESIAN_POINT('Ctrl Pts',(-20.7262541483525,-18.2359503350921,
10.1318398744086));
#164452=CARTESIAN_POINT('Ctrl Pts',(-20.7225805600179,-18.2258895701625,
10.1325349275789));
#164453=CARTESIAN_POINT('Origin',(-18.734,-18.952,0.));
#164454=CARTESIAN_POINT('',(-20.7225806572512,-18.2258898364529,11.1558809418218));
#164455=CARTESIAN_POINT('',(-20.7225805737622,-18.2258896078036,10.9336112541758));
#164456=CARTESIAN_POINT('',(-20.7225805737622,-18.2258896078036,0.));
#164457=CARTESIAN_POINT('',(-20.8509995968923,-18.9533064294668,11.1109437209282));
#164458=CARTESIAN_POINT('Ctrl Pts',(-20.7225806572512,-18.2258898364528,
11.1558809418218));
#164459=CARTESIAN_POINT('Ctrl Pts',(-20.7445653490361,-18.2860987896308,
11.1523876980793));
#164460=CARTESIAN_POINT('Ctrl Pts',(-20.7638236207115,-18.3473280257859,
11.148866803256));
#164461=CARTESIAN_POINT('Ctrl Pts',(-20.7906145474701,-18.4483623738006,
11.1430185087508));
#164462=CARTESIAN_POINT('Ctrl Pts',(-20.7998318209922,-18.4876155904459,
11.1407374682932));
#164463=CARTESIAN_POINT('Ctrl Pts',(-20.8091426747966,-18.5330622494928,
11.1380746906879));
#164464=CARTESIAN_POINT('Ctrl Pts',(-20.810337182083,-18.5390231667149,
11.1377250092448));
#164465=CARTESIAN_POINT('Ctrl Pts',(-20.8121465830655,-18.5482588933868,
11.1371825191121));
#164466=CARTESIAN_POINT('Ctrl Pts',(-20.8127794549061,-18.5515301764636,
11.1369902339572));
#164467=CARTESIAN_POINT('Ctrl Pts',(-20.8188276134209,-18.5831934728326,
11.1351277156095));
#164468=CARTESIAN_POINT('Ctrl Pts',(-20.823668421393,-18.6116910202044,
11.1334407929339));
#164469=CARTESIAN_POINT('Ctrl Pts',(-20.8294677003248,-18.6506463745914,
11.1311168585548));
#164470=CARTESIAN_POINT('Ctrl Pts',(-20.8309342166764,-18.6610261599489,
11.1304959174231));
#164471=CARTESIAN_POINT('Ctrl Pts',(-20.8331379335402,-18.6775064847892,
11.1295071452202));
#164472=CARTESIAN_POINT('Ctrl Pts',(-20.8339257801148,-18.6836001663461,
11.1291409180549));
#164473=CARTESIAN_POINT('Ctrl Pts',(-20.8354516398553,-18.6958202156194,
11.1284052142221));
#164474=CARTESIAN_POINT('Ctrl Pts',(-20.8361894177609,-18.7019465513535,
11.128035733981));
#164475=CARTESIAN_POINT('Ctrl Pts',(-20.8376163916899,-18.7142486771566,
11.1272924615129));
#164476=CARTESIAN_POINT('Ctrl Pts',(-20.8383052007869,-18.7204244495701,
11.1269186609687));
#164477=CARTESIAN_POINT('Ctrl Pts',(-20.8398173182982,-18.7345460163079,
11.1260623577006));
#164478=CARTESIAN_POINT('Ctrl Pts',(-20.8406228592429,-18.7424935818593,
11.125579299856));
#164479=CARTESIAN_POINT('Ctrl Pts',(-20.8425678107231,-18.7628293077294,
11.1243403135426));
#164480=CARTESIAN_POINT('Ctrl Pts',(-20.8436430278982,-18.7752231697907,
11.1235823826888));
#164481=CARTESIAN_POINT('Ctrl Pts',(-20.8489047513537,-18.8427850253306,
11.1194349460567));
#164482=CARTESIAN_POINT('Ctrl Pts',(-20.8510362032082,-18.8980864433055,
11.1159820573408));
#164483=CARTESIAN_POINT('Ctrl Pts',(-20.850999534888,-18.9534033118454,
11.1124694222872));
#164484=CARTESIAN_POINT('Ctrl Pts',(-20.7225805737622,-18.2258896078036,
10.3555828745111));
#164485=CARTESIAN_POINT('Ctrl Pts',(-20.6978476781926,-18.1581542383733,
10.3599055518532));
#164486=CARTESIAN_POINT('Ctrl Pts',(-20.6696396795271,-18.091656105465,
10.3642282291954));
#164487=CARTESIAN_POINT('Ctrl Pts',(-20.6381130015161,-18.0267742559477,
10.3685509065375));
#164488=CARTESIAN_POINT('Ctrl Pts',(-20.6065862617782,-17.9618922793962,
10.3728735923432));
#164489=CARTESIAN_POINT('Ctrl Pts',(-20.5717410483334,-17.8986270362431,
10.3771962781488));
#164490=CARTESIAN_POINT('Ctrl Pts',(-20.5337805560412,-17.837334601732,
10.3815189639545));
#164491=CARTESIAN_POINT('Ctrl Pts',(-20.4957820527404,-17.7759807932207,
10.3858459781984));
#164492=CARTESIAN_POINT('Ctrl Pts',(-20.4546623064218,-17.7166041567963,
10.3901729924423));
#164493=CARTESIAN_POINT('Ctrl Pts',(-20.4106682665917,-17.6595323896498,
10.3945000066862));
#164494=CARTESIAN_POINT('Ctrl Pts',(-20.3666496648147,-17.6024287592391,
10.3988294367095));
#164495=CARTESIAN_POINT('Ctrl Pts',(-20.3197538997825,-17.54763293286,10.4031588667328));
#164496=CARTESIAN_POINT('Ctrl Pts',(-20.270266850603,-17.495437895681,10.4074882967561));
#164497=CARTESIAN_POINT('Ctrl Pts',(-20.2206957041927,-17.4431541593742,
10.41182508412));
#164498=CARTESIAN_POINT('Ctrl Pts',(-20.1685248454057,-17.3934803710856,
10.4161618714839));
#164499=CARTESIAN_POINT('Ctrl Pts',(-20.1140747903873,-17.3466705718334,
10.4204986588478));
#164500=CARTESIAN_POINT('Ctrl Pts',(-20.0868591706488,-17.3232737599101,
10.4226663032283));
#164501=CARTESIAN_POINT('Ctrl Pts',(-20.0590746273095,-17.3005917894749,
10.4248339476089));
#164502=CARTESIAN_POINT('Ctrl Pts',(-20.0307638001156,-17.2786522636613,
10.4270015919895));
#164503=CARTESIAN_POINT('Ctrl Pts',(-19.9734509743369,-17.2342375875375,
10.4313898009204));
#164504=CARTESIAN_POINT('Ctrl Pts',(-19.9137418045022,-17.1926841015565,
10.4357780098513));
#164505=CARTESIAN_POINT('Ctrl Pts',(-19.8519537768686,-17.1542602099344,
10.4401662187822));
#164506=CARTESIAN_POINT('Ctrl Pts',(-19.7902574529128,-17.1158933457383,
10.4445479148834));
#164507=CARTESIAN_POINT('Ctrl Pts',(-19.7264888022834,-17.0806471078962,
10.4489296109847));
#164508=CARTESIAN_POINT('Ctrl Pts',(-19.6609970987602,-17.0487487346937,
10.453311307086));
#164509=CARTESIAN_POINT('Ctrl Pts',(-19.5955823532006,-17.0168878446182,
10.4576878543456));
#164510=CARTESIAN_POINT('Ctrl Pts',(-19.5284490083957,-16.9883672144277,
10.4620644016052));
#164511=CARTESIAN_POINT('Ctrl Pts',(-19.4599724698898,-16.9633690707016,
10.4664409488649));
#164512=CARTESIAN_POINT('Ctrl Pts',(-19.3915393582094,-16.938386780435,
10.4708147205818));
#164513=CARTESIAN_POINT('Ctrl Pts',(-19.3217651949897,-16.9169227092788,
10.4751884922988));
#164514=CARTESIAN_POINT('Ctrl Pts',(-19.2510456730811,-16.8991111155379,
10.4795622640158));
#164515=CARTESIAN_POINT('Ctrl Pts',(-19.1803476713603,-16.8813049419248,
10.4839347047793));
#164516=CARTESIAN_POINT('Ctrl Pts',(-19.108705349564,-16.8671491568768,
10.4883071455429));
#164517=CARTESIAN_POINT('Ctrl Pts',(-19.0365282611611,-16.8567277858954,
10.4926795863065));
#164518=CARTESIAN_POINT('Ctrl Pts',(-18.9643493271821,-16.8463061484384,
10.4970521388738));
#164519=CARTESIAN_POINT('Ctrl Pts',(-18.8916360771606,-16.8396191815878,
10.5014246914411));
#164520=CARTESIAN_POINT('Ctrl Pts',(-18.818805252056,-16.8366992957918,
10.5057972440085));
#164521=CARTESIAN_POINT('Ctrl Pts',(-18.745898840374,-16.8337763796282,
10.5101743345758));
#164522=CARTESIAN_POINT('Ctrl Pts',(-18.6728750930018,-16.8346283697016,
10.5145514251431));
#164523=CARTESIAN_POINT('Ctrl Pts',(-18.6001519939616,-16.8392355286782,
10.5189285157105));
#164524=CARTESIAN_POINT('Ctrl Pts',(-18.5273891781379,-16.8438452037953,
10.5233079967694));
#164525=CARTESIAN_POINT('Ctrl Pts',(-18.4549278170817,-16.8522140756297,
10.5276874778284));
#164526=CARTESIAN_POINT('Ctrl Pts',(-18.3831792948531,-16.8642706514397,
10.5320669588873));
#164527=CARTESIAN_POINT('Ctrl Pts',(-18.3113035988504,-16.8763485974493,
10.536454202547));
#164528=CARTESIAN_POINT('Ctrl Pts',(-18.2401437361919,-16.892127195905,
10.5408414462067));
#164529=CARTESIAN_POINT('Ctrl Pts',(-18.1700988737757,-16.9114842515082,
10.5452286898665));
#164530=CARTESIAN_POINT('Ctrl Pts',(-18.1224751168397,-16.9246451840769,
10.5482115928013));
#164531=CARTESIAN_POINT('Ctrl Pts',(-18.0753664841788,-16.9394592758344,
10.5511944957361));
#164532=CARTESIAN_POINT('Ctrl Pts',(-18.0288930166916,-16.9558754692931,
10.5541773986709));
#164533=CARTESIAN_POINT('Ctrl Pts',(-17.9605249572761,-16.9800256640268,
10.5585656076018));
#164534=CARTESIAN_POINT('Ctrl Pts',(-17.8932656103903,-17.0077395128394,
10.5629538165327));
#164535=CARTESIAN_POINT('Ctrl Pts',(-17.8275125107935,-17.0388953421435,
10.5673420254636));
#164536=CARTESIAN_POINT('Ctrl Pts',(-17.7618569996984,-17.0700049310313,
10.5717237215648));
#164537=CARTESIAN_POINT('Ctrl Pts',(-17.6977037303936,-17.1045461545567,
10.5761054176661));
#164538=CARTESIAN_POINT('Ctrl Pts',(-17.6354328295885,-17.1423483285189,
10.5804871137674));
#164539=CARTESIAN_POINT('Ctrl Pts',(-17.5732351020476,-17.1801060819184,
10.584863661027));
#164540=CARTESIAN_POINT('Ctrl Pts',(-17.5129157592867,-17.2211169246315,
10.5892402082867));
#164541=CARTESIAN_POINT('Ctrl Pts',(-17.4548312249221,-17.2651638357962,
10.5936167555463));
#164542=CARTESIAN_POINT('Ctrl Pts',(-17.3967835269251,-17.30918281305,10.5979905272633));
#164543=CARTESIAN_POINT('Ctrl Pts',(-17.3409682086665,-17.3562337476984,
10.6023642989803));
#164544=CARTESIAN_POINT('Ctrl Pts',(-17.2877123411689,-17.4060565961482,
10.6067380706972));
#164545=CARTESIAN_POINT('Ctrl Pts',(-17.2344726796106,-17.455864283338,
10.6111105114608));
#164546=CARTESIAN_POINT('Ctrl Pts',(-17.1837912746026,-17.5084418803646,
10.6154829522243));
#164547=CARTESIAN_POINT('Ctrl Pts',(-17.1359604618193,-17.5634904989842,
10.6198553929879));
#164548=CARTESIAN_POINT('Ctrl Pts',(-17.0881284259966,-17.6185405252032,
10.6242279455552));
#164549=CARTESIAN_POINT('Ctrl Pts',(-17.0431474419898,-17.6760613330222,
10.6286004981226));
#164550=CARTESIAN_POINT('Ctrl Pts',(-17.001270335834,-17.735720052406,10.63297305069));
#164551=CARTESIAN_POINT('Ctrl Pts',(-16.959349768038,-17.7954406878589,
10.6373501412573));
#164552=CARTESIAN_POINT('Ctrl Pts',(-16.9205397874117,-17.8573032692078,
10.6417272318246));
#164553=CARTESIAN_POINT('Ctrl Pts',(-16.8850500448045,-17.920945654593,
10.6461043223919));
#164554=CARTESIAN_POINT('Ctrl Pts',(-16.8495409199317,-17.984622797447,
10.6504838034509));
#164555=CARTESIAN_POINT('Ctrl Pts',(-16.8173558563404,-18.0500812464321,
10.6548632845098));
#164556=CARTESIAN_POINT('Ctrl Pts',(-16.788657414338,-18.1169363949914,
10.6592427655688));
#164557=CARTESIAN_POINT('Ctrl Pts',(-16.7599081045399,-18.1839100438526,
10.6636300092285));
#164558=CARTESIAN_POINT('Ctrl Pts',(-16.7346579248204,-18.2522848831352,
10.6680172528882));
#164559=CARTESIAN_POINT('Ctrl Pts',(-16.7130201897422,-18.3216591346498,
10.6724044965479));
#164560=CARTESIAN_POINT('Ctrl Pts',(-16.6983086148962,-18.3688269407928,
10.6753873994828));
#164561=CARTESIAN_POINT('Ctrl Pts',(-16.68526591231,-18.4164564326548,10.6783703024176));
#164562=CARTESIAN_POINT('Ctrl Pts',(-16.673914126578,-18.4644190383875,
10.6813532053524));
#164563=CARTESIAN_POINT('Ctrl Pts',(-16.6572142846389,-18.5349777992407,
10.6857414142833));
#164564=CARTESIAN_POINT('Ctrl Pts',(-16.6441110368839,-18.6065332466769,
10.6901296232142));
#164565=CARTESIAN_POINT('Ctrl Pts',(-16.6347172531062,-18.6786852572695,
10.6945178321451));
#164566=CARTESIAN_POINT('Ctrl Pts',(-16.6253374112611,-18.7507301823154,
10.6988995282463));
#164567=CARTESIAN_POINT('Ctrl Pts',(-16.6196561660671,-18.8233694384938,
10.7032812243476));
#164568=CARTESIAN_POINT('Ctrl Pts',(-16.6177357545009,-18.8961910112779,
10.7076629204489));
#164569=CARTESIAN_POINT('Ctrl Pts',(-16.6158175995711,-18.9689270129187,
10.7120394677085));
#164570=CARTESIAN_POINT('Ctrl Pts',(-16.6176515119966,-19.0418444257662,
10.7164160149681));
#164571=CARTESIAN_POINT('Ctrl Pts',(-16.6232479369201,-19.1145260846876,
10.7207925622278));
#164572=CARTESIAN_POINT('Ctrl Pts',(-16.6288408126722,-19.1871616499573,
10.7251663339447));
#164573=CARTESIAN_POINT('Ctrl Pts',(-16.6381914295875,-19.2595612781808,
10.7295401056617));
#164574=CARTESIAN_POINT('Ctrl Pts',(-16.6512581694981,-19.3313091977234,
10.7339138773787));
#164575=CARTESIAN_POINT('Ctrl Pts',(-16.6643209331558,-19.4030352841331,
10.7382863181422));
#164576=CARTESIAN_POINT('Ctrl Pts',(-16.6810974883881,-19.474109581296,
10.7426587589058));
#164577=CARTESIAN_POINT('Ctrl Pts',(-16.7014947532379,-19.5441244986356,
10.7470311996693));
#164578=CARTESIAN_POINT('Ctrl Pts',(-16.7218925396479,-19.6141412062643,
10.7514037522366));
#164579=CARTESIAN_POINT('Ctrl Pts',(-16.7459110826473,-19.6830980177226,
10.755776304804));
#164580=CARTESIAN_POINT('Ctrl Pts',(-16.7734073411518,-19.7506021700889,
10.7601488573713));
#164581=CARTESIAN_POINT('Ctrl Pts',(-16.8009321363106,-19.8181763808109,
10.7645259479386));
#164582=CARTESIAN_POINT('Ctrl Pts',(-16.8319416708358,-19.8842944746724,
10.7689030385059));
#164583=CARTESIAN_POINT('Ctrl Pts',(-16.8662449207617,-19.9485841479673,
10.7732801290733));
#164584=CARTESIAN_POINT('Ctrl Pts',(-16.9005669049657,-20.0129089322389,
10.7776596101322));
#164585=CARTESIAN_POINT('Ctrl Pts',(-16.938185937054,-20.0754028942404,
10.7820390911911));
#164586=CARTESIAN_POINT('Ctrl Pts',(-16.9788666145888,-20.1357211662445,
10.7864185722501));
#164587=CARTESIAN_POINT('Ctrl Pts',(-17.0196193983515,-20.1961463519807,
10.7908058159098));
#164588=CARTESIAN_POINT('Ctrl Pts',(-17.0634443742606,-20.2543877608696,
10.7951930595695));
#164589=CARTESIAN_POINT('Ctrl Pts',(-17.1100650454653,-20.3101326383827,
10.7995803032292));
#164590=CARTESIAN_POINT('Ctrl Pts',(-17.1417626095276,-20.3480337835284,
10.8025632061641));
#164591=CARTESIAN_POINT('Ctrl Pts',(-17.1747517071179,-20.3847815729316,
10.8055461090989));
#164592=CARTESIAN_POINT('Ctrl Pts',(-17.2089361619795,-20.4202878770739,
10.8085290120338));
#164593=CARTESIAN_POINT('Ctrl Pts',(-17.259225605987,-20.4725219203344,
10.8129172209647));
#164594=CARTESIAN_POINT('Ctrl Pts',(-17.3122998738987,-20.5222712846034,
10.8173054298956));
#164595=CARTESIAN_POINT('Ctrl Pts',(-17.3678836195123,-20.5692244850246,
10.8216936388265));
#164596=CARTESIAN_POINT('Ctrl Pts',(-17.4233848696315,-20.6161079991116,
10.8260753349277));
#164597=CARTESIAN_POINT('Ctrl Pts',(-17.4813878383961,-20.6602032789002,
10.830457031029));
#164598=CARTESIAN_POINT('Ctrl Pts',(-17.5415797744867,-20.7012349772934,
10.8348387271303));
#164599=CARTESIAN_POINT('Ctrl Pts',(-17.601700980262,-20.7422184601755,
10.8392152743899));
#164600=CARTESIAN_POINT('Ctrl Pts',(-17.6640056470489,-20.7801452426348,
10.8435918216496));
#164601=CARTESIAN_POINT('Ctrl Pts',(-17.7281486587465,-20.8147807383851,
10.8479683689092));
#164602=CARTESIAN_POINT('Ctrl Pts',(-17.7922509918783,-20.8493942688073,
10.8523421406262));
#164603=CARTESIAN_POINT('Ctrl Pts',(-17.8581889333125,-20.8807204253386,
10.8567159123431));
#164604=CARTESIAN_POINT('Ctrl Pts',(-17.9255903577767,-20.9085691529717,
10.8610896840601));
#164605=CARTESIAN_POINT('Ctrl Pts',(-17.992971271761,-20.9364094061434,
10.8654621248237));
#164606=CARTESIAN_POINT('Ctrl Pts',(-18.0618143390785,-20.9607741471641,
10.8698345655872));
#164607=CARTESIAN_POINT('Ctrl Pts',(-18.1317264570587,-20.9815210221806,
10.8742070063508));
#164608=CARTESIAN_POINT('Ctrl Pts',(-18.2016403626996,-21.002268427697,
10.8785795589181));
#164609=CARTESIAN_POINT('Ctrl Pts',(-18.2726229102622,-21.0193976482243,
10.8829521114855));
#164610=CARTESIAN_POINT('Ctrl Pts',(-18.3442664228595,-21.0328163635576,
10.8873246640528));
#164611=CARTESIAN_POINT('Ctrl Pts',(-18.4159842897964,-21.0462490053399,
10.8917017546201));
#164612=CARTESIAN_POINT('Ctrl Pts',(-18.488364016215,-21.0559633643478,
10.8960788451875));
#164613=CARTESIAN_POINT('Ctrl Pts',(-18.5609891559669,-21.0619185405714,
10.9004559357548));
#164614=CARTESIAN_POINT('Ctrl Pts',(-18.6336539590032,-21.0678769691378,
10.9048354168137));
#164615=CARTESIAN_POINT('Ctrl Pts',(-18.7065639597306,-21.070072112832,
10.9092148978727));
#164616=CARTESIAN_POINT('Ctrl Pts',(-18.7793017600921,-21.0685152374912,
10.9135943789316));
#164617=CARTESIAN_POINT('Ctrl Pts',(-18.8521684877164,-21.0669556025994,
10.9179816225913));
#164618=CARTESIAN_POINT('Ctrl Pts',(-18.9248619239424,-21.0616307033084,
10.9223688662511));
#164619=CARTESIAN_POINT('Ctrl Pts',(-18.996969429205,-21.052603741619,10.9267561099108));
#164620=CARTESIAN_POINT('Ctrl Pts',(-19.0459955845206,-21.0464662775061,
10.9297390128456));
#164621=CARTESIAN_POINT('Ctrl Pts',(-19.0947510327821,-21.0386185484977,
10.9327219157804));
#164622=CARTESIAN_POINT('Ctrl Pts',(-19.1431096126278,-21.0290937207684,
10.9357048187152));
#164623=CARTESIAN_POINT('Ctrl Pts',(-19.2142508990198,-21.0150815537551,
10.9400930276461));
#164624=CARTESIAN_POINT('Ctrl Pts',(-19.2848103359499,-20.9973828809338,
10.944481236577));
#164625=CARTESIAN_POINT('Ctrl Pts',(-19.3543769742706,-20.9760606240414,
10.9488694455079));
#164626=CARTESIAN_POINT('Ctrl Pts',(-19.4238403641657,-20.9547700129135,
10.9532511416092));
#164627=CARTESIAN_POINT('Ctrl Pts',(-19.4923134231176,-20.9298666339678,
10.9576328377105));
#164628=CARTESIAN_POINT('Ctrl Pts',(-19.5593953414347,-20.9014644214086,
10.9620145338117));
#164629=CARTESIAN_POINT('Ctrl Pts',(-19.6263984331591,-20.8730955837095,
10.9663910810714));
#164630=CARTESIAN_POINT('Ctrl Pts',(-19.6920131895943,-20.8412362668758,
10.970767628331));
#164631=CARTESIAN_POINT('Ctrl Pts',(-19.7558555559977,-20.8060496818254,
10.9751441755906));
#164632=CARTESIAN_POINT('Ctrl Pts',(-19.8196574345001,-20.7708854115958,
10.9795179473076));
#164633=CARTESIAN_POINT('Ctrl Pts',(-19.8816887317575,-20.7323982921379,
10.9838917190246));
#164634=CARTESIAN_POINT('Ctrl Pts',(-19.9415882172335,-20.6907983487451,
10.9882654907416));
#164635=CARTESIAN_POINT('Ctrl Pts',(-20.0014694750949,-20.6492110643549,
10.9926379315051));
#164636=CARTESIAN_POINT('Ctrl Pts',(-20.0592198131162,-20.6045131115933,
10.9970103722687));
#164637=CARTESIAN_POINT('Ctrl Pts',(-20.1145067552154,-20.5569579741553,
11.0013828130322));
#164638=CARTESIAN_POINT('Ctrl Pts',(-20.1697951110076,-20.5094016207273,
11.0057553655995));
#164639=CARTESIAN_POINT('Ctrl Pts',(-20.2226195814182,-20.4589882536492,
11.0101279181669));
#164640=CARTESIAN_POINT('Ctrl Pts',(-20.2726818719978,-20.4060106934907,
11.0145004707342));
#164641=CARTESIAN_POINT('Ctrl Pts',(-20.3227961191111,-20.3529781512218,
11.0188775613015));
#164642=CARTESIAN_POINT('Ctrl Pts',(-20.3701421308265,-20.2973764539275,
11.0232546518688));
#164643=CARTESIAN_POINT('Ctrl Pts',(-20.4144601023065,-20.2395336285146,
11.0276317424362));
#164644=CARTESIAN_POINT('Ctrl Pts',(-20.4588022774756,-20.181659212988,
11.0320112234951));
#164645=CARTESIAN_POINT('Ctrl Pts',(-20.5001128464796,-20.1215416302817,
11.036390704554));
#164646=CARTESIAN_POINT('Ctrl Pts',(-20.5381753524531,-20.0595379440908,
11.040770185613));
#164647=CARTESIAN_POINT('Ctrl Pts',(-20.5763053239628,-19.9974243567824,
11.0451574292727));
#164648=CARTESIAN_POINT('Ctrl Pts',(-20.6111755046318,-19.9334184139106,
11.0495446729324));
#164649=CARTESIAN_POINT('Ctrl Pts',(-20.6426156833703,-19.8679012900924,
11.0539319165921));
#164650=CARTESIAN_POINT('Ctrl Pts',(-20.6639919753443,-19.8233559591105,
11.056914819527));
#164651=CARTESIAN_POINT('Ctrl Pts',(-20.6837836766023,-19.7781125159706,
11.0598977224618));
#164652=CARTESIAN_POINT('Ctrl Pts',(-20.7019503858964,-19.7322949946336,
11.0628806253966));
#164653=CARTESIAN_POINT('Ctrl Pts',(-20.7321363776461,-19.6561641280754,
11.0678370477142));
#164654=CARTESIAN_POINT('Ctrl Pts',(-20.7579328257802,-19.5781989207149,
11.0727934700317));
#164655=CARTESIAN_POINT('Ctrl Pts',(-20.7791414399036,-19.4988870914449,
11.0777498923493));
#164656=CARTESIAN_POINT('Ctrl Pts',(-20.8002681015214,-19.4198817321354,
11.0826871624853));
#164657=CARTESIAN_POINT('Ctrl Pts',(-20.8168421753552,-19.339540355719,
11.0876244326213));
#164658=CARTESIAN_POINT('Ctrl Pts',(-20.8287143558559,-19.2583670468105,
11.0925617027573));
#164659=CARTESIAN_POINT('Ctrl Pts',(-20.8405099564276,-19.1777173355875,
11.0974671256858));
#164660=CARTESIAN_POINT('Ctrl Pts',(-20.8476640072491,-19.0962466252352,
11.1023725486143));
#164661=CARTESIAN_POINT('Ctrl Pts',(-20.8500781623711,-19.014467677533,
11.1072779715428));
#164662=CARTESIAN_POINT('Ctrl Pts',(-20.8506795164088,-18.9940969482639,
11.1084998880046));
#164663=CARTESIAN_POINT('Ctrl Pts',(-20.8509870073137,-18.9737071731892,
11.1097218044664));
#164664=CARTESIAN_POINT('Ctrl Pts',(-20.8509995968923,-18.9533064294668,
11.1109437209282));
#164665=CARTESIAN_POINT('',(-20.8509995968923,-18.9506935705329,10.8890562790718));
#164666=CARTESIAN_POINT('Ctrl Pts',(-20.7225805600179,-18.2258895701625,
10.1325349275789));
#164667=CARTESIAN_POINT('Ctrl Pts',(-20.6722698958125,-18.088105006425,
10.1420538457234));
#164668=CARTESIAN_POINT('Ctrl Pts',(-20.6077706502394,-17.9559073673189,
10.1518904366065));
#164669=CARTESIAN_POINT('Ctrl Pts',(-20.4974380565785,-17.7790617276431,
10.1654299361682));
#164670=CARTESIAN_POINT('Ctrl Pts',(-20.4624923458656,-17.7281480080467,
10.1693726022095));
#164671=CARTESIAN_POINT('Ctrl Pts',(-20.4198756844308,-17.6715330590799,
10.1737463730103));
#164672=CARTESIAN_POINT('Ctrl Pts',(-20.4143358467208,-17.6642718224488,
10.1743071185396));
#164673=CARTESIAN_POINT('Ctrl Pts',(-20.4059911886323,-17.6534797680504,
10.1751399143807));
#164674=CARTESIAN_POINT('Ctrl Pts',(-20.4032218823126,-17.6499218010714,
10.1754143728493));
#164675=CARTESIAN_POINT('Ctrl Pts',(-20.3982421186946,-17.6435658654405,
10.1759044412346));
#164676=CARTESIAN_POINT('Ctrl Pts',(-20.3960359481097,-17.6407646199431,
10.1761203480514));
#164677=CARTESIAN_POINT('Ctrl Pts',(-20.3912401600177,-17.6347068046313,
10.1765870757212));
#164678=CARTESIAN_POINT('Ctrl Pts',(-20.3886480248973,-17.6314523011539,
10.1768377124984));
#164679=CARTESIAN_POINT('Ctrl Pts',(-20.3813738002108,-17.6223743398601,
10.1775365908366));
#164680=CARTESIAN_POINT('Ctrl Pts',(-20.376670395407,-17.6165679315093,
10.1779833313244));
#164681=CARTESIAN_POINT('Ctrl Pts',(-20.3490476777093,-17.5828341155106,
10.1805779934644));
#164682=CARTESIAN_POINT('Ctrl Pts',(-20.3254457425266,-17.5554703653355,
10.1826795335719));
#164683=CARTESIAN_POINT('Ctrl Pts',(-20.24702547635,-17.4691227784648,10.1893509179404));
#164684=CARTESIAN_POINT('Ctrl Pts',(-20.1895372441879,-17.4126545856934,
10.1937780147657));
#164685=CARTESIAN_POINT('Ctrl Pts',(-20.0272905113737,-17.2705243031735,
10.2055350940063));
#164686=CARTESIAN_POINT('Ctrl Pts',(-19.9173219580414,-17.1914011543586,
10.212786593459));
#164687=CARTESIAN_POINT('Ctrl Pts',(-19.7460915794008,-17.091533388075,
10.2239369731859));
#164688=CARTESIAN_POINT('Ctrl Pts',(-19.6902328207078,-17.0622161322878,
10.227550613479));
#164689=CARTESIAN_POINT('Ctrl Pts',(-19.621846285762,-17.0301326941873,
10.2319867652531));
#164690=CARTESIAN_POINT('Ctrl Pts',(-19.6104934592948,-17.0249286017124,
10.2327235424176));
#164691=CARTESIAN_POINT('Ctrl Pts',(-19.5917883367819,-17.0165537294021,
10.2339383079784));
#164692=CARTESIAN_POINT('Ctrl Pts',(-19.5844628210791,-17.0133236256764,
10.2344142570031));
#164693=CARTESIAN_POINT('Ctrl Pts',(-19.5712677593889,-17.0075945912745,
10.2352720066905));
#164694=CARTESIAN_POINT('Ctrl Pts',(-19.5654048801239,-17.0050804797521,
10.235653283083));
#164695=CARTESIAN_POINT('Ctrl Pts',(-19.552902804297,-16.9997861271749,
10.2364666969055));
#164696=CARTESIAN_POINT('Ctrl Pts',(-19.5462606255731,-16.9970131759301,
10.2368990764962));
#164697=CARTESIAN_POINT('Ctrl Pts',(-19.5283563830478,-16.9896455771835,
10.2380652387579));
#164698=CARTESIAN_POINT('Ctrl Pts',(-19.5170687757731,-16.9851140788629,
10.2388011455585));
#164699=CARTESIAN_POINT('Ctrl Pts',(-19.4607285948192,-16.9630577206836,
10.2424782923465));
#164700=CARTESIAN_POINT('Ctrl Pts',(-19.4151270607714,-16.9469834991392,
10.2454676788553));
#164701=CARTESIAN_POINT('Ctrl Pts',(-19.2825598929839,-16.9052989597354,
10.2542017552102));
#164702=CARTESIAN_POINT('Ctrl Pts',(-19.1944542502738,-16.8836958992287,
10.2600638150178));
#164703=CARTESIAN_POINT('Ctrl Pts',(-18.9466725317166,-16.8395601520931,
10.2765862455825));
#164704=CARTESIAN_POINT('Ctrl Pts',(-18.7853924176671,-16.829502754587,
10.2874125079016));
#164705=CARTESIAN_POINT('Ctrl Pts',(-18.6045470186046,-16.8388669619853,
10.2987725610644));
#164706=CARTESIAN_POINT('Ctrl Pts',(-18.5845808398868,-16.8401848346858,
10.3000153438669));
#164707=CARTESIAN_POINT('Ctrl Pts',(-18.5582739519772,-16.84229620884,10.3016351049439));
#164708=CARTESIAN_POINT('Ctrl Pts',(-18.5519146187816,-16.8428355572064,
10.3020252934116));
#164709=CARTESIAN_POINT('Ctrl Pts',(-18.5416540709389,-16.843752527851,
10.3026525347584));
#164710=CARTESIAN_POINT('Ctrl Pts',(-18.5377513528179,-16.8441122351258,
10.3028905726005));
#164711=CARTESIAN_POINT('Ctrl Pts',(-18.5302454883645,-16.8448250651861,
10.3033473066581));
#164712=CARTESIAN_POINT('Ctrl Pts',(-18.5266422456396,-16.8451765928858,
10.3035660868237));
#164713=CARTESIAN_POINT('Ctrl Pts',(-18.5181199735707,-16.8460300898083,
10.3040824375918));
#164714=CARTESIAN_POINT('Ctrl Pts',(-18.5132017326801,-16.846540056253,
10.3043795592571));
#164715=CARTESIAN_POINT('Ctrl Pts',(-18.4968937250302,-16.8482887855668,
10.3053620191345));
#164716=CARTESIAN_POINT('Ctrl Pts',(-18.4855120018367,-16.8496027998366,
10.3060432596486));
#164717=CARTESIAN_POINT('Ctrl Pts',(-18.3863820814095,-16.8618635767563,
10.3119421836834));
#164718=CARTESIAN_POINT('Ctrl Pts',(-18.2993781328926,-16.8782073210213,
10.3168859421917));
#164719=CARTESIAN_POINT('Ctrl Pts',(-18.1191969458372,-16.9238974976155,
10.3270941912273));
#164720=CARTESIAN_POINT('Ctrl Pts',(-18.0265165640879,-16.9543387867889,
10.332330621597));
#164721=CARTESIAN_POINT('Ctrl Pts',(-17.8257067310208,-17.0360309412018,
10.3441890971973));
#164722=CARTESIAN_POINT('Ctrl Pts',(-17.7191682471214,-17.0902682509176,
10.3508437354321));
#164723=CARTESIAN_POINT('Ctrl Pts',(-17.6044270454248,-17.1614691647971,
10.3587543846365));
#164724=CARTESIAN_POINT('Ctrl Pts',(-17.5911731047225,-17.1698994419165,
10.3596798221563));
#164725=CARTESIAN_POINT('Ctrl Pts',(-17.5712616922301,-17.1828777316155,
10.3610884326554));
#164726=CARTESIAN_POINT('Ctrl Pts',(-17.5645341859119,-17.1873176830426,
10.3615675737536));
#164727=CARTESIAN_POINT('Ctrl Pts',(-17.5525237270254,-17.1953430672374,
10.3624288249267));
#164728=CARTESIAN_POINT('Ctrl Pts',(-17.5472313030677,-17.1989142001527,
10.3628103928089));
#164729=CARTESIAN_POINT('Ctrl Pts',(-17.5360350484277,-17.2065429556181,
10.3636220262905));
#164730=CARTESIAN_POINT('Ctrl Pts',(-17.5301355085513,-17.2106067063289,
10.3640523216783));
#164731=CARTESIAN_POINT('Ctrl Pts',(-17.5144013886891,-17.2215629304622,
10.3652070469168));
#164732=CARTESIAN_POINT('Ctrl Pts',(-17.5046047509211,-17.2285092003234,
10.3659335294753));
#164733=CARTESIAN_POINT('Ctrl Pts',(-17.457180036748,-17.2627456105679,
10.3694876167285));
#164734=CARTESIAN_POINT('Ctrl Pts',(-17.4204010254147,-17.2911848955679,
10.3723595748265));
#164735=CARTESIAN_POINT('Ctrl Pts',(-17.2543809878062,-17.4285257944055,
10.3858828288633));
#164736=CARTESIAN_POINT('Ctrl Pts',(-17.1375539378973,-17.5514326334662,
10.3971043873977));
#164737=CARTESIAN_POINT('Ctrl Pts',(-16.9772917657285,-17.7664563697633,
10.4147714372532));
#164738=CARTESIAN_POINT('Ctrl Pts',(-16.9236474072575,-17.8501081331215,
10.4212384656095));
#164739=CARTESIAN_POINT('Ctrl Pts',(-16.8714188430713,-17.9457324311004,
10.4279703856484));
#164740=CARTESIAN_POINT('Ctrl Pts',(-16.8668301438752,-17.9542727211565,
10.4285660569338));
#164741=CARTESIAN_POINT('Ctrl Pts',(-16.8601417705764,-17.9669285938369,
10.4294402619331));
#164742=CARTESIAN_POINT('Ctrl Pts',(-16.8579967152668,-17.9710198698124,
10.4297215614841));
#164743=CARTESIAN_POINT('Ctrl Pts',(-16.8542150737047,-17.9782903840641,
10.4302190959633));
#164744=CARTESIAN_POINT('Ctrl Pts',(-16.8525731348201,-17.9814667769973,
10.4304356657734));
#164745=CARTESIAN_POINT('Ctrl Pts',(-16.8490725670424,-17.9882810263389,
10.4308985543064));
#164746=CARTESIAN_POINT('Ctrl Pts',(-16.8472164226835,-17.991920096696,
10.4311447168412));
#164747=CARTESIAN_POINT('Ctrl Pts',(-16.8421505126772,-18.0019235167467,
10.431818609706));
#164748=CARTESIAN_POINT('Ctrl Pts',(-16.8389623039613,-18.0082988075681,
10.4322450080803));
#164749=CARTESIAN_POINT('Ctrl Pts',(-16.8221168459389,-18.0424133997934,
10.4345109315879));
#164750=CARTESIAN_POINT('Ctrl Pts',(-16.8090355584501,-18.0704348556229,
10.4363167328191));
#164751=CARTESIAN_POINT('Ctrl Pts',(-16.7713065040379,-18.1561025858176,
10.4417010775681));
#164752=CARTESIAN_POINT('Ctrl Pts',(-16.7485995112676,-18.2145689859085,
10.445192914413));
#164753=CARTESIAN_POINT('Ctrl Pts',(-16.6854703523919,-18.4012902075537,
10.456025536414));
#164754=CARTESIAN_POINT('Ctrl Pts',(-16.65464547695,-18.5324282384631,10.4631933055997));
#164755=CARTESIAN_POINT('Ctrl Pts',(-16.6309427723183,-18.7060252921972,
10.4729167940072));
#164756=CARTESIAN_POINT('Ctrl Pts',(-16.626593581554,-18.7465950294605,
10.4752036207267));
#164757=CARTESIAN_POINT('Ctrl Pts',(-16.6196346571376,-18.8357518755165,
10.4802860732568));
#164758=CARTESIAN_POINT('Ctrl Pts',(-16.6175223170951,-18.8843530252401,
10.4830935736719));
#164759=CARTESIAN_POINT('Ctrl Pts',(-16.6169721783228,-18.9455871747464,
10.486695070223));
#164760=CARTESIAN_POINT('Ctrl Pts',(-16.6169715281791,-18.9581936451916,
10.4874399163679));
#164761=CARTESIAN_POINT('Ctrl Pts',(-16.617148912416,-18.9781683387249,
10.4886257726986));
#164762=CARTESIAN_POINT('Ctrl Pts',(-16.6172528319408,-18.9855370446611,
10.4890644584691));
#164763=CARTESIAN_POINT('Ctrl Pts',(-16.6175181386771,-18.9992651874869,
10.4898840780203));
#164764=CARTESIAN_POINT('Ctrl Pts',(-16.6176697203885,-19.0056247469814,
10.4902646998807));
#164765=CARTESIAN_POINT('Ctrl Pts',(-16.6180700260682,-19.0197470848625,
10.4911120401309));
#164766=CARTESIAN_POINT('Ctrl Pts',(-16.6183328100806,-19.0275093443341,
10.491579194487));
#164767=CARTESIAN_POINT('Ctrl Pts',(-16.619220365993,-19.0500565280489,
10.4929403550887));
#164768=CARTESIAN_POINT('Ctrl Pts',(-16.6199574445897,-19.0648363397659,
10.4938378668877));
#164769=CARTESIAN_POINT('Ctrl Pts',(-16.6270369902696,-19.1820725058894,
10.5010001774815));
#164770=CARTESIAN_POINT('Ctrl Pts',(-16.6406680022971,-19.2839370731793,
10.5074949742385));
#164771=CARTESIAN_POINT('Ctrl Pts',(-16.6931329952607,-19.5353872176744,
10.5241676617908));
#164772=CARTESIAN_POINT('Ctrl Pts',(-16.741039872768,-19.6824690138303,
10.5345293706769));
#164773=CARTESIAN_POINT('Ctrl Pts',(-16.8267781797308,-19.872394814259,
10.548004025483));
#164774=CARTESIAN_POINT('Ctrl Pts',(-16.8509477519544,-19.9208844078065,
10.5514482833337));
#164775=CARTESIAN_POINT('Ctrl Pts',(-16.8811561096825,-19.9760777169471,
10.5553298831095));
#164776=CARTESIAN_POINT('Ctrl Pts',(-16.8854072393869,-19.9837317789636,
10.5558672718623));
#164777=CARTESIAN_POINT('Ctrl Pts',(-16.8919105706579,-19.9952716332977,
10.5566758566068));
#164778=CARTESIAN_POINT('Ctrl Pts',(-16.8941277931071,-19.9991768855835,
10.5569492098837));
#164779=CARTESIAN_POINT('Ctrl Pts',(-16.8981271548686,-20.0061691522531,
10.5574380922266));
#164780=CARTESIAN_POINT('Ctrl Pts',(-16.8999046715142,-20.0092587344969,
10.5576539120312));
#164781=CARTESIAN_POINT('Ctrl Pts',(-16.903780660933,-20.0159565748604,
10.5581213519162));
#164782=CARTESIAN_POINT('Ctrl Pts',(-16.9058819975309,-20.0195631091523,
10.5583727830689));
#164783=CARTESIAN_POINT('Ctrl Pts',(-16.911805962269,-20.0296616568609,
10.5590761238205));
#164784=CARTESIAN_POINT('Ctrl Pts',(-16.9156526423605,-20.0361395890955,
10.5595265011856));
#164785=CARTESIAN_POINT('Ctrl Pts',(-16.9386800343948,-20.0744511048151,
10.5621862115086));
#164786=CARTESIAN_POINT('Ctrl Pts',(-16.9586630301275,-20.1057977662017,
10.5643464045908));
#164787=CARTESIAN_POINT('Ctrl Pts',(-17.0267137532656,-20.2065888709176,
10.5712945173517));
#164788=CARTESIAN_POINT('Ctrl Pts',(-17.0781140338294,-20.2736896301121,
10.5759257334966));
#164789=CARTESIAN_POINT('Ctrl Pts',(-17.2506581557071,-20.4730162841514,
10.5902792368159));
#164790=CARTESIAN_POINT('Ctrl Pts',(-17.3846355336124,-20.5930370498418,
10.5998939651431));
#164791=CARTESIAN_POINT('Ctrl Pts',(-17.5508115398299,-20.7076393325562,
10.6116272333925));
#164792=CARTESIAN_POINT('Ctrl Pts',(-17.5697060862666,-20.7202262361048,
10.6129575213388));
#164793=CARTESIAN_POINT('Ctrl Pts',(-17.5967877348927,-20.7376448382678,
10.614860577841));
#164794=CARTESIAN_POINT('Ctrl Pts',(-17.6048109811919,-20.7427292870994,
10.6154239303715));
#164795=CARTESIAN_POINT('Ctrl Pts',(-17.6179222192687,-20.7509149197118,
10.6163439252608));
#164796=CARTESIAN_POINT('Ctrl Pts',(-17.6229896219742,-20.7540489559957,
10.6166993495682));
#164797=CARTESIAN_POINT('Ctrl Pts',(-17.6336402254532,-20.7605740342824,
10.6174461013302));
#164798=CARTESIAN_POINT('Ctrl Pts',(-17.6392260183593,-20.7639607055782,
10.6178375841665));
#164799=CARTESIAN_POINT('Ctrl Pts',(-17.6525808019803,-20.7719734270524,
10.6187732325132));
#164800=CARTESIAN_POINT('Ctrl Pts',(-17.6603638841503,-20.7765756338942,
10.619318260011));
#164801=CARTESIAN_POINT('Ctrl Pts',(-17.6868238543261,-20.7919937301016,
10.6211704423554));
#164802=CARTESIAN_POINT('Ctrl Pts',(-17.7056360977903,-20.8025735428203,
10.6224860725914));
#164803=CARTESIAN_POINT('Ctrl Pts',(-17.8098762366445,-20.8591168286656,
10.6297718146139));
#164804=CARTESIAN_POINT('Ctrl Pts',(-17.8982128622423,-20.8994482620257,
10.6359383220046));
#164805=CARTESIAN_POINT('Ctrl Pts',(-18.121404318156,-20.9833607784153,
10.6514460292614));
#164806=CARTESIAN_POINT('Ctrl Pts',(-18.2584637581474,-21.0197433723829,
10.6609235987738));
#164807=CARTESIAN_POINT('Ctrl Pts',(-18.4591174948786,-21.0519869038313,
10.6741249126858));
#164808=CARTESIAN_POINT('Ctrl Pts',(-18.5205181290289,-21.0591147097923,
10.6780715520071));
#164809=CARTESIAN_POINT('Ctrl Pts',(-18.5912594754872,-21.064202070666,
10.6824491631104));
#164810=CARTESIAN_POINT('Ctrl Pts',(-18.6003750853159,-21.0647983419468,
10.6830100260713));
#164811=CARTESIAN_POINT('Ctrl Pts',(-18.6139956483926,-21.0656007869646,
10.6838429615622));
#164812=CARTESIAN_POINT('Ctrl Pts',(-18.6184977255407,-21.065851592834,
10.6841174434136));
#164813=CARTESIAN_POINT('Ctrl Pts',(-18.6265614269687,-21.0662749743925,
10.6846075369578));
#164814=CARTESIAN_POINT('Ctrl Pts',(-18.6301227040379,-21.0664529368859,
10.684823445681));
#164815=CARTESIAN_POINT('Ctrl Pts',(-18.6378401379202,-21.0668190440643,
10.6852901585808));
#164816=CARTESIAN_POINT('Ctrl Pts',(-18.6419963916222,-21.0670039349708,
10.6855407787833));
#164817=CARTESIAN_POINT('Ctrl Pts',(-18.6536176828466,-21.0674865864939,
10.6862395641056));
#164818=CARTESIAN_POINT('Ctrl Pts',(-18.6610838763265,-21.0677570884272,
10.6866862287983));
#164819=CARTESIAN_POINT('Ctrl Pts',(-18.7046408023064,-21.0691043251046,
10.6892795575349));
#164820=CARTESIAN_POINT('Ctrl Pts',(-18.740755245574,-21.069297192962,10.6913798956955));
#164821=CARTESIAN_POINT('Ctrl Pts',(-18.8572742825499,-21.0669377469551,
10.6980456916112));
#164822=CARTESIAN_POINT('Ctrl Pts',(-18.9375377343523,-21.0607277292522,
10.702468676844));
#164823=CARTESIAN_POINT('Ctrl Pts',(-19.2007449267228,-21.0251905831569,
10.7169459827154));
#164824=CARTESIAN_POINT('Ctrl Pts',(-19.3801672616446,-20.9764584051596,
10.7268511112178));
#164825=CARTESIAN_POINT('Ctrl Pts',(-19.571394849294,-20.8964663667563,
10.7389062784494));
#164826=CARTESIAN_POINT('Ctrl Pts',(-19.5916922970075,-20.887598991046,
10.7402046340292));
#164827=CARTESIAN_POINT('Ctrl Pts',(-19.6195497484071,-20.8749046540006,
10.7420142327873));
#164828=CARTESIAN_POINT('Ctrl Pts',(-19.6272319532677,-20.871348154916,
10.7425162042258));
#164829=CARTESIAN_POINT('Ctrl Pts',(-19.6403943259379,-20.8651584590622,
10.7433814166704));
#164830=CARTESIAN_POINT('Ctrl Pts',(-19.6458848998638,-20.8625475371704,
10.7437438846988));
#164831=CARTESIAN_POINT('Ctrl Pts',(-19.657058947053,-20.8571748237869,
10.7444847614002));
#164832=CARTESIAN_POINT('Ctrl Pts',(-19.6627414502739,-20.8544111664218,
10.7448632322053));
#164833=CARTESIAN_POINT('Ctrl Pts',(-19.6758282027507,-20.8479738802264,
10.7457388236822));
#164834=CARTESIAN_POINT('Ctrl Pts',(-19.6832234443535,-20.8442822642674,
10.7462365696697));
#164835=CARTESIAN_POINT('Ctrl Pts',(-19.698752716199,-20.836416297489,10.7472881003529));
#164836=CARTESIAN_POINT('Ctrl Pts',(-19.7068816860658,-20.8322323809728,
10.7478422145986));
#164837=CARTESIAN_POINT('Ctrl Pts',(-19.7284727436111,-20.8209421304386,
10.7493239179516));
#164838=CARTESIAN_POINT('Ctrl Pts',(-19.7418855258113,-20.8137431274456,
10.7502547604062));
#164839=CARTESIAN_POINT('Ctrl Pts',(-19.7826080439514,-20.7913172142988,
10.7531131738256));
#164840=CARTESIAN_POINT('Ctrl Pts',(-19.8096581337974,-20.7756299139956,
10.755056821481));
#164841=CARTESIAN_POINT('Ctrl Pts',(-19.9115933758983,-20.7134569534753,
10.7625562930663));
#164842=CARTESIAN_POINT('Ctrl Pts',(-19.9838897543784,-20.6629147966443,
10.768249228799));
#164843=CARTESIAN_POINT('Ctrl Pts',(-20.1501754307354,-20.5304883149296,
10.7821903337796));
#164844=CARTESIAN_POINT('Ctrl Pts',(-20.2405030026954,-20.4445237217131,
10.7905059498207));
#164845=CARTESIAN_POINT('Ctrl Pts',(-20.3265463925974,-20.3468182249581,
10.7989321283601));
#164846=CARTESIAN_POINT('Ctrl Pts',(-20.3303193418767,-20.3424986346499,
10.7993026986361));
#164847=CARTESIAN_POINT('Ctrl Pts',(-20.3456139976044,-20.32484372755,10.8008091845524));
#164848=CARTESIAN_POINT('Ctrl Pts',(-20.3569868081859,-20.3113797962197,
10.8019393528701));
#164849=CARTESIAN_POINT('Ctrl Pts',(-20.3899140874462,-20.2713958151356,
10.8052375596493));
#164850=CARTESIAN_POINT('Ctrl Pts',(-20.4109972825622,-20.2444926318388,
10.8073832829217));
#164851=CARTESIAN_POINT('Ctrl Pts',(-20.4355884802939,-20.2114976279042,
10.8099164130435));
#164852=CARTESIAN_POINT('Ctrl Pts',(-20.4397282118522,-20.2058855216293,
10.8103439275266));
#164853=CARTESIAN_POINT('Ctrl Pts',(-20.4464704608535,-20.1966500792647,
10.8110418530585));
#164854=CARTESIAN_POINT('Ctrl Pts',(-20.4490893537915,-20.1930388424476,
10.8113133619646));
#164855=CARTESIAN_POINT('Ctrl Pts',(-20.4537791936258,-20.1865287427941,
10.8118002790251));
#164856=CARTESIAN_POINT('Ctrl Pts',(-20.4558542443182,-20.1836329215729,
10.8120159676145));
#164857=CARTESIAN_POINT('Ctrl Pts',(-20.460358134635,-20.1773139220428,
10.8124846598887));
#164858=CARTESIAN_POINT('Ctrl Pts',(-20.4627840992379,-20.1738887655987,
10.8127374663054));
#164859=CARTESIAN_POINT('Ctrl Pts',(-20.4695975818573,-20.1642080741141,
10.8134485538441));
#164860=CARTESIAN_POINT('Ctrl Pts',(-20.4739614946099,-20.1579358948144,
10.8139052479421));
#164861=CARTESIAN_POINT('Ctrl Pts',(-20.5004231915003,-20.1194602633663,
10.8166831680809));
#164862=CARTESIAN_POINT('Ctrl Pts',(-20.5216618107861,-20.0866717784964,
10.8189500255668));
#164863=CARTESIAN_POINT('Ctrl Pts',(-20.6270022752281,-19.9137383238074,
10.8304965834505));
#164864=CARTESIAN_POINT('Ctrl Pts',(-20.6955814745115,-19.7647772513501,
10.8391212131246));
#164865=CARTESIAN_POINT('Ctrl Pts',(-20.7656532888853,-19.5502820287956,
10.8515090133897));
#164866=CARTESIAN_POINT('Ctrl Pts',(-20.7823497632473,-19.4903483736763,
10.8549621547645));
#164867=CARTESIAN_POINT('Ctrl Pts',(-20.8079993458133,-19.3796270822072,
10.8614076387259));
#164868=CARTESIAN_POINT('Ctrl Pts',(-20.8177820311267,-19.3290809298379,
10.8643744138636));
#164869=CARTESIAN_POINT('Ctrl Pts',(-20.8276939265967,-19.2655283584958,
10.8681560229178));
#164870=CARTESIAN_POINT('Ctrl Pts',(-20.8295593324667,-19.252807850628,
10.8689154551197));
#164871=CARTESIAN_POINT('Ctrl Pts',(-20.8323193599981,-19.232713419598,
10.8701193860392));
#164872=CARTESIAN_POINT('Ctrl Pts',(-20.8332912550207,-19.2253502970991,
10.8705614382008));
#164873=CARTESIAN_POINT('Ctrl Pts',(-20.8349476974874,-19.2122708513839,
10.8713483300385));
#164874=CARTESIAN_POINT('Ctrl Pts',(-20.8356477136965,-19.2065565362713,
10.8716926770491));
#164875=CARTESIAN_POINT('Ctrl Pts',(-20.8370323024389,-19.1948588156978,
10.8723987589714));
#164876=CARTESIAN_POINT('Ctrl Pts',(-20.8377146681132,-19.1888752065147,
10.8727605602234));
#164877=CARTESIAN_POINT('Ctrl Pts',(-20.8391674074184,-19.1756346206786,
10.8735625742349));
#164878=CARTESIAN_POINT('Ctrl Pts',(-20.8399258046106,-19.1683764317348,
10.8740031604327));
#164879=CARTESIAN_POINT('Ctrl Pts',(-20.8417118990209,-19.1503830876938,
10.8750977751567));
#164880=CARTESIAN_POINT('Ctrl Pts',(-20.8426951156183,-19.139643815158,
10.8757531931529));
#164881=CARTESIAN_POINT('Ctrl Pts',(-20.8485694989575,-19.0695887482446,
10.8800427237244));
#164882=CARTESIAN_POINT('Ctrl Pts',(-20.8510389800155,-19.0101025990038,
10.8837519461892));
#164883=CARTESIAN_POINT('Ctrl Pts',(-20.8509995348883,-18.9505966887089,
10.8875305864451));
#164884=CARTESIAN_POINT('Ctrl Pts',(-20.7225805737622,-18.2258896078036,
10.9336112541758));
#164885=CARTESIAN_POINT('Ctrl Pts',(-20.7506609300752,-18.3027925851862,
10.9286590766383));
#164886=CARTESIAN_POINT('Ctrl Pts',(-20.774308399499,-18.3814140088411,
10.9237068991007));
#164887=CARTESIAN_POINT('Ctrl Pts',(-20.7933360861973,-18.4612618986816,
10.9187547215632));
#164888=CARTESIAN_POINT('Ctrl Pts',(-20.8123544087724,-18.5410704928639,
10.9138049811479));
#164889=CARTESIAN_POINT('Ctrl Pts',(-20.8267573247981,-18.6221041354718,
10.9088552407327));
#164890=CARTESIAN_POINT('Ctrl Pts',(-20.8364059167827,-18.7038501237617,
10.9039055003175));
#164891=CARTESIAN_POINT('Ctrl Pts',(-20.8460545087673,-18.7855961120516,
10.8989557599023));
#164892=CARTESIAN_POINT('Ctrl Pts',(-20.8509485990149,-18.8680542176316,
10.894006019487));
#164893=CARTESIAN_POINT('Ctrl Pts',(-20.8509995968923,-18.9506935705329,
10.8890562790718));
#164894=CARTESIAN_POINT('Origin',(-18.734,-18.952,0.));
#164895=CARTESIAN_POINT('',(-20.7225805737639,-18.2258896078082,11.9535388216361));
#164896=CARTESIAN_POINT('',(-20.7219729293148,-18.2261210096956,11.7337477406533));
#164897=CARTESIAN_POINT('',(-20.7225805737622,-18.2258896078036,0.));
#164898=CARTESIAN_POINT('Ctrl Pts',(-20.7225805737639,-18.2258896078082,
11.9535388216361));
#164899=CARTESIAN_POINT('Ctrl Pts',(-20.7228709312506,-18.2266848026764,
11.9534867202617));
#164900=CARTESIAN_POINT('Ctrl Pts',(-20.7231608131558,-18.227480175522,
11.9534346446637));
#164901=CARTESIAN_POINT('Ctrl Pts',(-20.725902506219,-18.2350168328669,
11.9529415517011));
#164902=CARTESIAN_POINT('Ctrl Pts',(-20.7283205553233,-18.2417704721402,
11.9525023862134));
#164903=CARTESIAN_POINT('Ctrl Pts',(-20.7320650323148,-18.2523987590967,
11.9518156428223));
#164904=CARTESIAN_POINT('Ctrl Pts',(-20.7334145990786,-18.2562651142276,
11.9515667258745));
#164905=CARTESIAN_POINT('Ctrl Pts',(-20.7359210084393,-18.2635132172769,
11.9511018196));
#164906=CARTESIAN_POINT('Ctrl Pts',(-20.7370804929103,-18.2668939402145,
11.9508856802641));
#164907=CARTESIAN_POINT('Ctrl Pts',(-20.7397139281656,-18.2746361153159,
11.9503922975431));
#164908=CARTESIAN_POINT('Ctrl Pts',(-20.741182214819,-18.2789994417947,
11.9501153908462));
#164909=CARTESIAN_POINT('Ctrl Pts',(-20.7456726548253,-18.2924891564348,
11.9492627605705));
#164910=CARTESIAN_POINT('Ctrl Pts',(-20.748646932759,-18.3016315143292,
11.9486897864207));
#164911=CARTESIAN_POINT('Ctrl Pts',(-20.7774525836471,-18.3922686854927,
11.9430545507576));
#164912=CARTESIAN_POINT('Ctrl Pts',(-20.7983905072509,-18.475247455487,
11.9382548304568));
#164913=CARTESIAN_POINT('Ctrl Pts',(-20.8385991713034,-18.6882312932793,
11.9263204505388));
#164914=CARTESIAN_POINT('Ctrl Pts',(-20.8509009167449,-18.8191722303356,
11.9193213968354));
#164915=CARTESIAN_POINT('Ctrl Pts',(-20.8510686213727,-19.0426470678854,
11.9069621000412));
#164916=CARTESIAN_POINT('Ctrl Pts',(-20.8451100146564,-19.1347783337778,
11.9017508967304));
#164917=CARTESIAN_POINT('Ctrl Pts',(-20.8313804901704,-19.2398780717802,
11.8955372391559));
#164918=CARTESIAN_POINT('Ctrl Pts',(-20.8294631847735,-19.2535173836545,
11.8947257424901));
#164919=CARTESIAN_POINT('Ctrl Pts',(-20.8261768229805,-19.2753482609065,
11.8934182636011));
#164920=CARTESIAN_POINT('Ctrl Pts',(-20.8248923983335,-19.2835523066434,
11.8929249583066));
#164921=CARTESIAN_POINT('Ctrl Pts',(-20.822527335613,-19.2980981837992,
11.8920467670036));
#164922=CARTESIAN_POINT('Ctrl Pts',(-20.8214659899728,-19.3044430787071,
11.8916624977564));
#164923=CARTESIAN_POINT('Ctrl Pts',(-20.8191956396849,-19.3176454991027,
11.8908603644548));
#164924=CARTESIAN_POINT('Ctrl Pts',(-20.8179816893291,-19.3245020852471,
11.8904423472302));
#164925=CARTESIAN_POINT('Ctrl Pts',(-20.814744118203,-19.3422771081671,
11.8893548950549));
#164926=CARTESIAN_POINT('Ctrl Pts',(-20.8126683981604,-19.3531857297131,
11.8886838073358));
#164927=CARTESIAN_POINT('Ctrl Pts',(-20.8033102385072,-19.4003426132209,
11.8857663337448));
#164928=CARTESIAN_POINT('Ctrl Pts',(-20.7951650843611,-19.4364111752216,
11.8834925737344));
#164929=CARTESIAN_POINT('Ctrl Pts',(-20.7710540925085,-19.5315155296063,
11.8773805295259));
#164930=CARTESIAN_POINT('Ctrl Pts',(-20.7534686094193,-19.5901011389758,
11.8734935544757));
#164931=CARTESIAN_POINT('Ctrl Pts',(-20.6816192014538,-19.7965478971811,
11.8593775533143));
#164932=CARTESIAN_POINT('Ctrl Pts',(-20.6134415276801,-19.939003132821,
11.8488054745441));
#164933=CARTESIAN_POINT('Ctrl Pts',(-20.4974380103206,-20.1249383399141,
11.834570067347));
#164934=CARTESIAN_POINT('Ctrl Pts',(-20.4624923195146,-20.175852027263,
11.8306274038046));
#164935=CARTESIAN_POINT('Ctrl Pts',(-20.4198756814308,-20.2324669448607,
11.8262536354274));
#164936=CARTESIAN_POINT('Ctrl Pts',(-20.4143358444966,-20.2397281804442,
11.8256928899791));
#164937=CARTESIAN_POINT('Ctrl Pts',(-20.4059911873827,-20.2505202335576,
11.8248600942372));
#164938=CARTESIAN_POINT('Ctrl Pts',(-20.40322188125,-20.2540782002897,11.8245856357877));
#164939=CARTESIAN_POINT('Ctrl Pts',(-20.3982421178699,-20.2604341356083,
11.8240955674265));
#164940=CARTESIAN_POINT('Ctrl Pts',(-20.3960359473336,-20.2632353810404,
11.8238796606147));
#164941=CARTESIAN_POINT('Ctrl Pts',(-20.3912401592339,-20.269293196355,
11.8234129329448));
#164942=CARTESIAN_POINT('Ctrl Pts',(-20.3886480240565,-20.2725476999,11.8231622961623));
#164943=CARTESIAN_POINT('Ctrl Pts',(-20.3813737989229,-20.2816256617391,
11.8224634177822));
#164944=CARTESIAN_POINT('Ctrl Pts',(-20.3766703937245,-20.2874320705638,
11.8220166772581));
#164945=CARTESIAN_POINT('Ctrl Pts',(-20.349047668151,-20.3211658960738,
11.8194220143871));
#164946=CARTESIAN_POINT('Ctrl Pts',(-20.3254457250298,-20.3485296549071,
11.817320473616));
#164947=CARTESIAN_POINT('Ctrl Pts',(-20.2470254196683,-20.4348772817698,
11.8106490861315));
#164948=CARTESIAN_POINT('Ctrl Pts',(-20.1895371530908,-20.4913455027572,
11.8062219870092));
#164949=CARTESIAN_POINT('Ctrl Pts',(-20.0272904009265,-20.6334757790618,
11.7944649073733));
#164950=CARTESIAN_POINT('Ctrl Pts',(-19.9173218706877,-20.7125989017598,
11.7872134095763));
#164951=CARTESIAN_POINT('Ctrl Pts',(-19.7460915352509,-20.8124666352626,
11.7760630327267));
#164952=CARTESIAN_POINT('Ctrl Pts',(-19.6902327937904,-20.8417838806634,
11.7724493935458));
#164953=CARTESIAN_POINT('Ctrl Pts',(-19.6218462783899,-20.8738673092074,
11.7680132430391));
#164954=CARTESIAN_POINT('Ctrl Pts',(-19.6104934534501,-20.8790714009349,
11.7672764659737));
#164955=CARTESIAN_POINT('Ctrl Pts',(-19.5917883330134,-20.8874462722656,
11.7660617005476));
#164956=CARTESIAN_POINT('Ctrl Pts',(-19.58446281785,-20.8906763757377,11.7655857515579));
#164957=CARTESIAN_POINT('Ctrl Pts',(-19.5712677568455,-20.8964054098201,
11.764728001915));
#164958=CARTESIAN_POINT('Ctrl Pts',(-19.5654048777231,-20.8989195212726,
11.7643467255317));
#164959=CARTESIAN_POINT('Ctrl Pts',(-19.5529028018915,-20.9042138738347,
11.7635333117088));
#164960=CARTESIAN_POINT('Ctrl Pts',(-19.5462606230191,-20.9069868251316,
11.7631009321083));
#164961=CARTESIAN_POINT('Ctrl Pts',(-19.5283563793399,-20.9143544243242,
11.7619347697713));
#164962=CARTESIAN_POINT('Ctrl Pts',(-19.5170687710539,-20.9188859230227,
11.7611988629045));
#164963=CARTESIAN_POINT('Ctrl Pts',(-19.4607285749817,-20.9409422869315,
11.757521715128));
#164964=CARTESIAN_POINT('Ctrl Pts',(-19.4151270264761,-20.957016512875,
11.7545323276651));
#164965=CARTESIAN_POINT('Ctrl Pts',(-19.2825598008812,-20.9987010669186,
11.745798247469));
#164966=CARTESIAN_POINT('Ctrl Pts',(-19.1944541136651,-21.0203041331306,
11.7399361846457));
#164967=CARTESIAN_POINT('Ctrl Pts',(-18.9466719648108,-21.0644399346196,
11.7234137253526));
#164968=CARTESIAN_POINT('Ctrl Pts',(-18.7853914552946,-21.074497298231,
11.7125874362613));
#164969=CARTESIAN_POINT('Ctrl Pts',(-18.604546034287,-21.0651329742962,
11.7012273863597));
#164970=CARTESIAN_POINT('Ctrl Pts',(-18.5845802163514,-21.0638151177757,
11.6999846263648));
#164971=CARTESIAN_POINT('Ctrl Pts',(-18.5582737333368,-21.0617037728127,
11.6983648903738));
#164972=CARTESIAN_POINT('Ctrl Pts',(-18.5519144449285,-21.0611644276489,
11.6979747046831));
#164973=CARTESIAN_POINT('Ctrl Pts',(-18.5416539518808,-21.060247461268,
11.6973474667173));
#164974=CARTESIAN_POINT('Ctrl Pts',(-18.5377512437939,-21.0598877547051,
11.6971094294979));
#164975=CARTESIAN_POINT('Ctrl Pts',(-18.5302453855069,-21.0591749248747,
11.6966526958337));
#164976=CARTESIAN_POINT('Ctrl Pts',(-18.52664213892,-21.0588233966174,11.6964339154428));
#164977=CARTESIAN_POINT('Ctrl Pts',(-18.5181198390236,-21.0579698964561,
11.6959175630112));
#164978=CARTESIAN_POINT('Ctrl Pts',(-18.5132015741813,-21.057459927182,
11.6956204399158));
#164979=CARTESIAN_POINT('Ctrl Pts',(-18.4968934055338,-21.0557111791746,
11.6946379704072));
#164980=CARTESIAN_POINT('Ctrl Pts',(-18.4855115455229,-21.0543971469823,
11.6939567218025));
#164981=CARTESIAN_POINT('Ctrl Pts',(-18.3830528668735,-21.0417246268513,
11.6878597145945));
#164982=CARTESIAN_POINT('Ctrl Pts',(-18.292782373007,-21.0245453062832,
11.6827394478474));
#164983=CARTESIAN_POINT('Ctrl Pts',(-18.0905383908386,-20.9722369445543,
11.6712834801344));
#164984=CARTESIAN_POINT('Ctrl Pts',(-17.9798030325778,-20.9335618779371,
11.6650138234529));
#164985=CARTESIAN_POINT('Ctrl Pts',(-17.7841420945091,-20.8464352044565,
11.6531957025434));
#164986=CARTESIAN_POINT('Ctrl Pts',(-17.6982834873898,-20.8008922787253,
11.647723227365));
#164987=CARTESIAN_POINT('Ctrl Pts',(-17.6040552742434,-20.7422813026597,
11.6412189246558));
#164988=CARTESIAN_POINT('Ctrl Pts',(-17.5923245977831,-20.734823459614,
11.6404000339324));
#164989=CARTESIAN_POINT('Ctrl Pts',(-17.57367366098,-20.7227064591146,11.6390829124332));
#164990=CARTESIAN_POINT('Ctrl Pts',(-17.5667058970322,-20.7181209051227,
11.6385874226187));
#164991=CARTESIAN_POINT('Ctrl Pts',(-17.554407978302,-20.7099229562399,
11.6377067127351));
#164992=CARTESIAN_POINT('Ctrl Pts',(-17.5490668339413,-20.7063271782335,
11.637322121584));
#164993=CARTESIAN_POINT('Ctrl Pts',(-17.5379977207763,-20.6988015916346,
11.6365206923166));
#164994=CARTESIAN_POINT('Ctrl Pts',(-17.5322725312649,-20.6948678497073,
11.6361037078559));
#164995=CARTESIAN_POINT('Ctrl Pts',(-17.5175084250336,-20.6846161910314,
11.6350219256616));
#164996=CARTESIAN_POINT('Ctrl Pts',(-17.5084994158515,-20.6782557540619,
11.6343555073403));
#164997=CARTESIAN_POINT('Ctrl Pts',(-17.470078750806,-20.6506780988765,
11.6314858721419));
#164998=CARTESIAN_POINT('Ctrl Pts',(-17.4411666651739,-20.6287784352367,
11.6292563809623));
#164999=CARTESIAN_POINT('Ctrl Pts',(-17.366328946895,-20.5690055797999,
11.6232932602904));
#165000=CARTESIAN_POINT('Ctrl Pts',(-17.3214159490521,-20.529921555662,
11.6195138303613));
#165001=CARTESIAN_POINT('Ctrl Pts',(-17.1558768544209,-20.3731292376476,
11.6048076785868));
#165002=CARTESIAN_POINT('Ctrl Pts',(-17.0478256862569,-20.2430808675952,
11.5934626031465));
#165003=CARTESIAN_POINT('Ctrl Pts',(-16.9272027772928,-20.0565592035218,
11.5791037003395));
#165004=CARTESIAN_POINT('Ctrl Pts',(-16.8997895125758,-20.0104139918105,
11.57569255942));
#165005=CARTESIAN_POINT('Ctrl Pts',(-16.8699806882701,-19.9555922688549,
11.571842977358));
#165006=CARTESIAN_POINT('Ctrl Pts',(-16.8658518619861,-19.9478855240929,
11.5713063541948));
#165007=CARTESIAN_POINT('Ctrl Pts',(-16.8596759196141,-19.9361841212052,
11.5704986914318));
#165008=CARTESIAN_POINT('Ctrl Pts',(-16.8575936268885,-19.9322082771287,
11.570225501732));
#165009=CARTESIAN_POINT('Ctrl Pts',(-16.8538803728326,-19.9250631486774,
11.5697367944129));
#165010=CARTESIAN_POINT('Ctrl Pts',(-16.8522447644358,-19.9218963541476,
11.5695209869676));
#165011=CARTESIAN_POINT('Ctrl Pts',(-16.8487101505957,-19.9150101883395,
11.5690534392953));
#165012=CARTESIAN_POINT('Ctrl Pts',(-16.8468141561918,-19.9112893362976,
11.5688018887232));
#165013=CARTESIAN_POINT('Ctrl Pts',(-16.8415244148065,-19.9008319435131,
11.5680978763587));
#165014=CARTESIAN_POINT('Ctrl Pts',(-16.8381556045682,-19.8940827616384,
11.5676469515149));
#165015=CARTESIAN_POINT('Ctrl Pts',(-16.8183324160605,-19.8538313792483,
11.5649772640497));
#165016=CARTESIAN_POINT('Ctrl Pts',(-16.8027292152315,-19.8199145519605,
11.5628080718355));
#165017=CARTESIAN_POINT('Ctrl Pts',(-16.7545367183236,-19.707413250753,
11.5558167842105));
#165018=CARTESIAN_POINT('Ctrl Pts',(-16.725783323603,-19.6272718910687,
11.551153630289));
#165019=CARTESIAN_POINT('Ctrl Pts',(-16.6519385130739,-19.3744840995508,
11.5368176931546));
#165020=CARTESIAN_POINT('Ctrl Pts',(-16.6237691651234,-19.1977480782823,
11.5272467262133));
#165021=CARTESIAN_POINT('Ctrl Pts',(-16.6173518026154,-18.996812513012,
11.5155621957774));
#165022=CARTESIAN_POINT('Ctrl Pts',(-16.616992205476,-18.9740384092867,
11.5142276513877));
#165023=CARTESIAN_POINT('Ctrl Pts',(-16.6170034365873,-18.9417527538923,
11.5123195573282));
#165024=CARTESIAN_POINT('Ctrl Pts',(-16.6170708372447,-18.9322421928686,
11.5117554928235));
#165025=CARTESIAN_POINT('Ctrl Pts',(-16.6172847240138,-18.9167726308347,
11.5108346546508));
#165026=CARTESIAN_POINT('Ctrl Pts',(-16.6173922965961,-18.9108131586095,
11.5104791035797));
#165027=CARTESIAN_POINT('Ctrl Pts',(-16.6176704649905,-18.898325571687,
11.5097323471504));
#165028=CARTESIAN_POINT('Ctrl Pts',(-16.6178461020897,-18.8917976422054,
11.5093409875668));
#165029=CARTESIAN_POINT('Ctrl Pts',(-16.6183366062704,-18.8762440375105,
11.5084061197012));
#165030=CARTESIAN_POINT('Ctrl Pts',(-16.6186790291309,-18.8672194145403,
11.5078617531892));
#165031=CARTESIAN_POINT('Ctrl Pts',(-16.6200326343453,-18.8367003582321,
11.5060141579507));
#165032=CARTESIAN_POINT('Ctrl Pts',(-16.6213137594955,-18.8152197895042,
11.5047025106788));
#165033=CARTESIAN_POINT('Ctrl Pts',(-16.6363972790706,-18.6139868128247,
11.4923054145702));
#165034=CARTESIAN_POINT('Ctrl Pts',(-16.6727791395181,-18.4367010598517,
11.4804684396029));
#165035=CARTESIAN_POINT('Ctrl Pts',(-16.7699001797035,-18.1530603222483,
11.4606622851455));
#165036=CARTESIAN_POINT('Ctrl Pts',(-16.8181667966911,-18.0433843038417,
11.4527932201824));
#165037=CARTESIAN_POINT('Ctrl Pts',(-16.88000589595,-17.9299992120614,11.4448159967796));
#165038=CARTESIAN_POINT('Ctrl Pts',(-16.8846236158346,-17.9216666821436,
11.4442308027965));
#165039=CARTESIAN_POINT('Ctrl Pts',(-16.8915477729611,-17.9093687958875,
11.4433689938721));
#165040=CARTESIAN_POINT('Ctrl Pts',(-16.8938110301694,-17.9053794417563,
11.4430897227625));
#165041=CARTESIAN_POINT('Ctrl Pts',(-16.8978601059011,-17.8982960325788,
11.4425944228796));
#165042=CARTESIAN_POINT('Ctrl Pts',(-16.8996408051028,-17.8951991169496,
11.4423780704635));
#165043=CARTESIAN_POINT('Ctrl Pts',(-16.9034851807604,-17.8885521369334,
11.4419141391035));
#165044=CARTESIAN_POINT('Ctrl Pts',(-16.9055513430801,-17.8850035751779,
11.4416667242589));
#165045=CARTESIAN_POINT('Ctrl Pts',(-16.9112808458405,-17.8752288687222,
11.4409858614255));
#165046=CARTESIAN_POINT('Ctrl Pts',(-16.9149657894449,-17.8690153609838,
11.4405537916633));
#165047=CARTESIAN_POINT('Ctrl Pts',(-16.9352893954879,-17.8351423353129,
11.4382017068095));
#165048=CARTESIAN_POINT('Ctrl Pts',(-16.9525281500796,-17.8078456458654,
11.436318527035));
#165049=CARTESIAN_POINT('Ctrl Pts',(-17.060495493342,-17.6452452935144,
11.4251087104377));
#165050=CARTESIAN_POINT('Ctrl Pts',(-17.1659769765886,-17.5203782157972,
11.4164988834854));
#165051=CARTESIAN_POINT('Ctrl Pts',(-17.3700049986271,-17.3287666348621,
11.4011763020977));
#165052=CARTESIAN_POINT('Ctrl Pts',(-17.4617397747621,-17.2559110975352,
11.3946470605129));
#165053=CARTESIAN_POINT('Ctrl Pts',(-17.570876237423,-17.1830920053328,
11.386960646138));
#165054=CARTESIAN_POINT('Ctrl Pts',(-17.5828186112244,-17.1752969364621,
11.386120807448));
#165055=CARTESIAN_POINT('Ctrl Pts',(-17.6019578968922,-17.1630782526814,
11.3847763998458));
#165056=CARTESIAN_POINT('Ctrl Pts',(-17.6091042323647,-17.1585759424942,
11.3842747571289));
#165057=CARTESIAN_POINT('Ctrl Pts',(-17.6217596106978,-17.1507082442188,
11.3833869128543));
#165058=CARTESIAN_POINT('Ctrl Pts',(-17.6272574932249,-17.1473250444158,
11.383001374589));
#165059=CARTESIAN_POINT('Ctrl Pts',(-17.6386650397899,-17.1403769827243,
11.3822017283011));
#165060=CARTESIAN_POINT('Ctrl Pts',(-17.6445768277832,-17.1368157719217,
11.3817874924848));
#165061=CARTESIAN_POINT('Ctrl Pts',(-17.6598051375919,-17.1277435581502,
11.3807208291417));
#165062=CARTESIAN_POINT('Ctrl Pts',(-17.6691466195901,-17.1222750372067,
11.3800668657194));
#165063=CARTESIAN_POINT('Ctrl Pts',(-17.708386380808,-17.099706280852,11.3773210252668));
#165064=CARTESIAN_POINT('Ctrl Pts',(-17.7386564142118,-17.0832661384781,
11.3752056077944));
#165065=CARTESIAN_POINT('Ctrl Pts',(-17.81863541282,-17.042322815823,11.3696200971174));
#165066=CARTESIAN_POINT('Ctrl Pts',(-17.8689267494071,-17.0190212850063,
11.3661110815783));
#165067=CARTESIAN_POINT('Ctrl Pts',(-18.0212914076408,-16.955563607542,
11.3554994428696));
#165068=CARTESIAN_POINT('Ctrl Pts',(-18.1256274505189,-16.9213372537294,
11.3482485731389));
#165069=CARTESIAN_POINT('Ctrl Pts',(-18.29350956687,-16.880370614754,11.3368339890718));
#165070=CARTESIAN_POINT('Ctrl Pts',(-18.3555262760965,-16.8681481787254,
11.332672471414));
#165071=CARTESIAN_POINT('Ctrl Pts',(-18.4213590370903,-16.8582100926892,
11.3283638131055));
#165072=CARTESIAN_POINT('Ctrl Pts',(-18.4247203799251,-16.8577109405697,
11.3281441181102));
#165073=CARTESIAN_POINT('Ctrl Pts',(-18.4797755059873,-16.849670811192,
11.3245508054879));
#165074=CARTESIAN_POINT('Ctrl Pts',(-18.5317346620249,-16.8440370436972,
11.3212320853524));
#165075=CARTESIAN_POINT('Ctrl Pts',(-18.5925033426384,-16.839716189436,
11.3174742935894));
#165076=CARTESIAN_POINT('Ctrl Pts',(-18.6011571902866,-16.8391542900071,
11.3169420802446));
#165077=CARTESIAN_POINT('Ctrl Pts',(-18.6142794835943,-16.8383831937566,
11.316139730426));
#165078=CARTESIAN_POINT('Ctrl Pts',(-18.618745420425,-16.8381349644739,
11.31586748503));
#165079=CARTESIAN_POINT('Ctrl Pts',(-18.6267705205871,-16.8377144148757,
11.3153797853612));
#165080=CARTESIAN_POINT('Ctrl Pts',(-18.6303293450097,-16.8375369256974,
11.3151640465357));
#165081=CARTESIAN_POINT('Ctrl Pts',(-18.6380718132848,-16.8371703802019,
11.3146958642062));
#165082=CARTESIAN_POINT('Ctrl Pts',(-18.6422555616313,-16.8369847526536,
11.3144436146022));
#165083=CARTESIAN_POINT('Ctrl Pts',(-18.6540307580913,-16.8364973078251,
11.3137356668708));
#165084=CARTESIAN_POINT('Ctrl Pts',(-18.6616234083277,-16.8362239359533,
11.3132815334538));
#165085=CARTESIAN_POINT('Ctrl Pts',(-18.707474970354,-16.8348201708283,
11.3105523638864));
#165086=CARTESIAN_POINT('Ctrl Pts',(-18.7457599095072,-16.834686578804,
11.308329506119));
#165087=CARTESIAN_POINT('Ctrl Pts',(-18.8728173637419,-16.8376901034067,
11.3010765949882));
#165088=CARTESIAN_POINT('Ctrl Pts',(-18.9613920415912,-16.8453742712031,
11.2962193926562));
#165089=CARTESIAN_POINT('Ctrl Pts',(-19.2202180231406,-16.884348779317,
11.2819832346259));
#165090=CARTESIAN_POINT('Ctrl Pts',(-19.3873884125689,-16.9309442580225,
11.272674686867));
#165091=CARTESIAN_POINT('Ctrl Pts',(-19.5684222982214,-17.0062442706738,
11.2612834044764));
#165092=CARTESIAN_POINT('Ctrl Pts',(-19.5896688836689,-17.0154937053638,
11.2599260374505));
#165093=CARTESIAN_POINT('Ctrl Pts',(-19.6194748279846,-17.0290556360585,
11.2579909361443));
#165094=CARTESIAN_POINT('Ctrl Pts',(-19.6281637658312,-17.0330805506472,
11.2574230619284));
#165095=CARTESIAN_POINT('Ctrl Pts',(-19.6422269228757,-17.0397111817477,
11.2564977074545));
#165096=CARTESIAN_POINT('Ctrl Pts',(-19.647618009958,-17.0422809634389,
11.2561414742079));
#165097=CARTESIAN_POINT('Ctrl Pts',(-19.6587540335295,-17.0476471437192,
11.2554024813631));
#165098=CARTESIAN_POINT('Ctrl Pts',(-19.6644973223784,-17.050446804475,
11.2550196109674));
#165099=CARTESIAN_POINT('Ctrl Pts',(-19.67800895145,-17.0571091412742,11.2541147126182));
#165100=CARTESIAN_POINT('Ctrl Pts',(-19.6857663512819,-17.0609936340756,
11.2535919252617));
#165101=CARTESIAN_POINT('Ctrl Pts',(-19.7021571666019,-17.069327688443,
11.2524802998627));
#165102=CARTESIAN_POINT('Ctrl Pts',(-19.7107842552369,-17.0737891902844,
11.2518910496806));
#165103=CARTESIAN_POINT('Ctrl Pts',(-19.7340897893561,-17.0860456524255,
11.2502877835504));
#165104=CARTESIAN_POINT('Ctrl Pts',(-19.7487074053523,-17.093954233381,
11.249269778892));
#165105=CARTESIAN_POINT('Ctrl Pts',(-19.7941068259137,-17.1192122365549,
11.2460685218741));
#165106=CARTESIAN_POINT('Ctrl Pts',(-19.8245471448638,-17.1371600171479,
11.2438644214309));
#165107=CARTESIAN_POINT('Ctrl Pts',(-19.9427199517914,-17.2108821895701,
11.2350763602771));
#165108=CARTESIAN_POINT('Ctrl Pts',(-20.0267351210617,-17.2723194690709,
11.2283027994222));
#165109=CARTESIAN_POINT('Ctrl Pts',(-20.2181072730451,-17.435153238626,
11.2117354014159));
#165110=CARTESIAN_POINT('Ctrl Pts',(-20.3200567163725,-17.5420961393826,
11.2018925055787));
#165111=CARTESIAN_POINT('Ctrl Pts',(-20.4195625264171,-17.6710593147378,
11.191733433425));
#165112=CARTESIAN_POINT('Ctrl Pts',(-20.4289121067432,-17.6834563262121,
11.190772937982));
#165113=CARTESIAN_POINT('Ctrl Pts',(-20.4415454570355,-17.7005964870405,
11.1894681003514));
#165114=CARTESIAN_POINT('Ctrl Pts',(-20.4449472322576,-17.70525150479,11.1891160338837));
#165115=CARTESIAN_POINT('Ctrl Pts',(-20.4503284718,-17.7126787425664,11.1885580386074));
#165116=CARTESIAN_POINT('Ctrl Pts',(-20.4523203065535,-17.7154419032232,
11.1883512650601));
#165117=CARTESIAN_POINT('Ctrl Pts',(-20.4564251791198,-17.7211654332352,
11.1879246694373));
#165118=CARTESIAN_POINT('Ctrl Pts',(-20.458537258717,-17.7241264430484,
11.1877049184263));
#165119=CARTESIAN_POINT('Ctrl Pts',(-20.4635596999673,-17.7312061281343,
11.1871817153378));
#165120=CARTESIAN_POINT('Ctrl Pts',(-20.4664630181722,-17.7353298206995,
11.1868787460013));
#165121=CARTESIAN_POINT('Ctrl Pts',(-20.4762414008545,-17.749324399551,
11.1858564246949));
#165122=CARTESIAN_POINT('Ctrl Pts',(-20.483047206855,-17.7592437038189,
11.1851416406802));
#165123=CARTESIAN_POINT('Ctrl Pts',(-20.499217713228,-17.7832478970739,
11.1834340304655));
#165124=CARTESIAN_POINT('Ctrl Pts',(-20.5084990254507,-17.7973882476143,
11.1824461894464));
#165125=CARTESIAN_POINT('Ctrl Pts',(-20.5428019498615,-17.8510405840154,
11.1787595408908));
#165126=CARTESIAN_POINT('Ctrl Pts',(-20.5666828365081,-17.8912689725686,
11.1761190721565));
#165127=CARTESIAN_POINT('Ctrl Pts',(-20.6411145223748,-18.0266822471018,
11.1675225730271));
#165128=CARTESIAN_POINT('Ctrl Pts',(-20.6856867898319,-18.12484947811,11.1617431696283));
#165129=CARTESIAN_POINT('Ctrl Pts',(-20.7225806572512,-18.2258898364528,
11.1558809418218));
#165130=CARTESIAN_POINT('',(-20.8510159085425,-18.9509245719999,11.689056243827));
#165131=CARTESIAN_POINT('Ctrl Pts',(-20.8509997268492,-18.9509245835809,
11.6890562436241));
#165132=CARTESIAN_POINT('Ctrl Pts',(-20.851036160924,-19.0226464998528,
11.6847206650332));
#165133=CARTESIAN_POINT('Ctrl Pts',(-20.8474235543286,-19.094516438247,
11.6803850864424));
#165134=CARTESIAN_POINT('Ctrl Pts',(-20.8401430852434,-19.1661268420388,
11.6760495078516));
#165135=CARTESIAN_POINT('Ctrl Pts',(-20.8328737172097,-19.2376280563309,
11.6717205400272));
#165136=CARTESIAN_POINT('Ctrl Pts',(-20.8219476405722,-19.3088700336357,
11.6673915722028));
#165137=CARTESIAN_POINT('Ctrl Pts',(-20.8073980430312,-19.3794453826564,
11.6630626043785));
#165138=CARTESIAN_POINT('Ctrl Pts',(-20.7928607647321,-19.4499609750556,
11.6587373019202));
#165139=CARTESIAN_POINT('Ctrl Pts',(-20.7747061465264,-19.519810575807,
11.6544119994619));
#165140=CARTESIAN_POINT('Ctrl Pts',(-20.7530189912495,-19.5885935225668,
11.6500866970037));
#165141=CARTESIAN_POINT('Ctrl Pts',(-20.7313426461036,-19.6573421839323,
11.645763550526));
#165142=CARTESIAN_POINT('Ctrl Pts',(-20.7061374043849,-19.7250247747427,
11.6414404040484));
#165143=CARTESIAN_POINT('Ctrl Pts',(-20.6775383611409,-19.7912542158213,
11.6371172575707));
#165144=CARTESIAN_POINT('Ctrl Pts',(-20.6489436148248,-19.8574737061077,
11.632794760634));
#165145=CARTESIAN_POINT('Ctrl Pts',(-20.6169562761289,-19.9222400264192,
11.6284722636973));
#165146=CARTESIAN_POINT('Ctrl Pts',(-20.5817594783951,-19.9851862900761,
11.6241497667606));
#165147=CARTESIAN_POINT('Ctrl Pts',(-20.546531034035,-20.0481891508387,
11.6198233833213));
#165148=CARTESIAN_POINT('Ctrl Pts',(-20.5080876068702,-20.1093682524657,
11.615496999882));
#165149=CARTESIAN_POINT('Ctrl Pts',(-20.466657721841,-20.1683824312052,
11.6111706164427));
#165150=CARTESIAN_POINT('Ctrl Pts',(-20.4252103606757,-20.2274215035649,
11.6068424080293));
#165151=CARTESIAN_POINT('Ctrl Pts',(-20.3807743381557,-20.2842934442376,
11.6025141996159));
#165152=CARTESIAN_POINT('Ctrl Pts',(-20.3336191165972,-20.3386894684164,
11.5981859912025));
#165153=CARTESIAN_POINT('Ctrl Pts',(-20.2863774057491,-20.3931852625322,
11.5938498442479));
#165154=CARTESIAN_POINT('Ctrl Pts',(-20.2364068762127,-20.4451957108582,
11.5895136972933));
#165155=CARTESIAN_POINT('Ctrl Pts',(-20.1840141561295,-20.4944486853779,
11.5851775503387));
#165156=CARTESIAN_POINT('Ctrl Pts',(-20.1349615139615,-20.5405617432795,
11.5811178362293));
#165157=CARTESIAN_POINT('Ctrl Pts',(-20.0837862726385,-20.5842578770899,
11.5770581221199));
#165158=CARTESIAN_POINT('Ctrl Pts',(-20.0307638001156,-20.6253477363387,
11.5729984080105));
#165159=CARTESIAN_POINT('Ctrl Pts',(-19.973450974337,-20.6697624124625,
11.5686101990796));
#165160=CARTESIAN_POINT('Ctrl Pts',(-19.9137418045024,-20.7113158984434,
11.5642219901487));
#165161=CARTESIAN_POINT('Ctrl Pts',(-19.8519537768689,-20.7497397900654,
11.5598337812178));
#165162=CARTESIAN_POINT('Ctrl Pts',(-19.790257452913,-20.7881066542616,
11.5554520851166));
#165163=CARTESIAN_POINT('Ctrl Pts',(-19.7264888022836,-20.8233528921037,
11.5510703890153));
#165164=CARTESIAN_POINT('Ctrl Pts',(-19.6609970987604,-20.8552512653062,
11.5466886929141));
#165165=CARTESIAN_POINT('Ctrl Pts',(-19.5955823532009,-20.8871121553817,
11.5423121456544));
#165166=CARTESIAN_POINT('Ctrl Pts',(-19.528449008396,-20.9156327855722,
11.5379355983948));
#165167=CARTESIAN_POINT('Ctrl Pts',(-19.4599724698901,-20.9406309292982,
11.5335590511351));
#165168=CARTESIAN_POINT('Ctrl Pts',(-19.3915393582098,-20.9656132195649,
11.5291852794182));
#165169=CARTESIAN_POINT('Ctrl Pts',(-19.3217651949901,-20.9870772907211,
11.5248115077012));
#165170=CARTESIAN_POINT('Ctrl Pts',(-19.2510456730815,-21.004888884462,
11.5204377359842));
#165171=CARTESIAN_POINT('Ctrl Pts',(-19.1803476713609,-21.0226950580751,
11.5160652952207));
#165172=CARTESIAN_POINT('Ctrl Pts',(-19.1087053495646,-21.0368508431231,
11.5116928544571));
#165173=CARTESIAN_POINT('Ctrl Pts',(-19.0365282611618,-21.0472722141045,
11.5073204136936));
#165174=CARTESIAN_POINT('Ctrl Pts',(-18.9643493271831,-21.0576938515615,
11.5029478611263));
#165175=CARTESIAN_POINT('Ctrl Pts',(-18.8916360771617,-21.0643808184121,
11.4985753085589));
#165176=CARTESIAN_POINT('Ctrl Pts',(-18.8188052520574,-21.0673007042082,
11.4942027559916));
#165177=CARTESIAN_POINT('Ctrl Pts',(-18.7458988403754,-21.0702236203718,
11.4898256654243));
#165178=CARTESIAN_POINT('Ctrl Pts',(-18.6728750930033,-21.0693716302984,
11.4854485748569));
#165179=CARTESIAN_POINT('Ctrl Pts',(-18.6001519939632,-21.0647644713219,
11.4810714842896));
#165180=CARTESIAN_POINT('Ctrl Pts',(-18.5273891781395,-21.0601547962048,
11.4766920032307));
#165181=CARTESIAN_POINT('Ctrl Pts',(-18.4549278170834,-21.0517859243705,
11.4723125221717));
#165182=CARTESIAN_POINT('Ctrl Pts',(-18.3831792948548,-21.0397293485606,
11.4679330411128));
#165183=CARTESIAN_POINT('Ctrl Pts',(-18.3113035988522,-21.0276514025511,
11.4635457974531));
#165184=CARTESIAN_POINT('Ctrl Pts',(-18.2401437361938,-21.0118728040954,
11.4591585537934));
#165185=CARTESIAN_POINT('Ctrl Pts',(-18.1700988737776,-20.9925157484923,
11.4547713101337));
#165186=CARTESIAN_POINT('Ctrl Pts',(-18.1224751168409,-20.9793548159235,
11.4517884071988));
#165187=CARTESIAN_POINT('Ctrl Pts',(-18.0753664841794,-20.9645407241658,
11.448805504264));
#165188=CARTESIAN_POINT('Ctrl Pts',(-18.0288930166914,-20.9481245307068,
11.4458226013291));
#165189=CARTESIAN_POINT('Ctrl Pts',(-17.9605249572759,-20.9239743359732,
11.4414343923982));
#165190=CARTESIAN_POINT('Ctrl Pts',(-17.89326561039,-20.8962604871604,11.4370461834673));
#165191=CARTESIAN_POINT('Ctrl Pts',(-17.8275125107931,-20.8651046578563,
11.4326579745364));
#165192=CARTESIAN_POINT('Ctrl Pts',(-17.7618569996981,-20.8339950689686,
11.4282762784351));
#165193=CARTESIAN_POINT('Ctrl Pts',(-17.6977037303935,-20.7994538454432,
11.4238945823339));
#165194=CARTESIAN_POINT('Ctrl Pts',(-17.6354328295885,-20.761651671481,
11.4195128862326));
#165195=CARTESIAN_POINT('Ctrl Pts',(-17.5732351020475,-20.7238939180816,
11.415136338973));
#165196=CARTESIAN_POINT('Ctrl Pts',(-17.5129157592866,-20.6828830753684,
11.4107597917133));
#165197=CARTESIAN_POINT('Ctrl Pts',(-17.4548312249219,-20.6388361642037,
11.4063832444537));
#165198=CARTESIAN_POINT('Ctrl Pts',(-17.3967835269248,-20.5948171869498,
11.4020094727367));
#165199=CARTESIAN_POINT('Ctrl Pts',(-17.3409682086662,-20.5477662523014,
11.3976357010197));
#165200=CARTESIAN_POINT('Ctrl Pts',(-17.2877123411685,-20.4979434038514,
11.3932619293027));
#165201=CARTESIAN_POINT('Ctrl Pts',(-17.2344726796102,-20.4481357166616,
11.3888894885392));
#165202=CARTESIAN_POINT('Ctrl Pts',(-17.1837912746022,-20.3955581196349,
11.3845170477756));
#165203=CARTESIAN_POINT('Ctrl Pts',(-17.1359604618188,-20.3405095010152,
11.3801446070121));
#165204=CARTESIAN_POINT('Ctrl Pts',(-17.0881284259963,-20.2854594747964,
11.3757720544447));
#165205=CARTESIAN_POINT('Ctrl Pts',(-17.0431474419896,-20.2279386669774,
11.3713995018774));
#165206=CARTESIAN_POINT('Ctrl Pts',(-17.0012703358339,-20.1682799475938,
11.36702694931));
#165207=CARTESIAN_POINT('Ctrl Pts',(-16.9593497680378,-20.1085593121409,
11.3626498587427));
#165208=CARTESIAN_POINT('Ctrl Pts',(-16.9205397874116,-20.046696730792,
11.3582727681754));
#165209=CARTESIAN_POINT('Ctrl Pts',(-16.8850500448044,-19.9830543454068,
11.353895677608));
#165210=CARTESIAN_POINT('Ctrl Pts',(-16.8495409199316,-19.9193772025528,
11.3495161965491));
#165211=CARTESIAN_POINT('Ctrl Pts',(-16.8173558563403,-19.8539187535678,
11.3451367154901));
#165212=CARTESIAN_POINT('Ctrl Pts',(-16.788657414338,-19.7870636050085,
11.3407572344312));
#165213=CARTESIAN_POINT('Ctrl Pts',(-16.7599081045398,-19.7200899561471,
11.3363699907715));
#165214=CARTESIAN_POINT('Ctrl Pts',(-16.7346579248203,-19.6517151168644,
11.3319827471118));
#165215=CARTESIAN_POINT('Ctrl Pts',(-16.7130201897421,-19.5823408653497,
11.327595503452));
#165216=CARTESIAN_POINT('Ctrl Pts',(-16.6983086148961,-19.5351730592069,
11.3246126005172));
#165217=CARTESIAN_POINT('Ctrl Pts',(-16.6852659123099,-19.487543567345,
11.3216296975824));
#165218=CARTESIAN_POINT('Ctrl Pts',(-16.673914126578,-19.4395809616125,
11.3186467946476));
#165219=CARTESIAN_POINT('Ctrl Pts',(-16.657214284639,-19.3690222007594,
11.3142585857167));
#165220=CARTESIAN_POINT('Ctrl Pts',(-16.6441110368839,-19.2974667533233,
11.3098703767858));
#165221=CARTESIAN_POINT('Ctrl Pts',(-16.6347172531062,-19.2253147427308,
11.3054821678549));
#165222=CARTESIAN_POINT('Ctrl Pts',(-16.6253374112611,-19.1532698176848,
11.3011004717537));
#165223=CARTESIAN_POINT('Ctrl Pts',(-16.6196561660671,-19.0806305615062,
11.2967187756524));
#165224=CARTESIAN_POINT('Ctrl Pts',(-16.6177357545009,-19.0078089887219,
11.2923370795511));
#165225=CARTESIAN_POINT('Ctrl Pts',(-16.6158175995711,-18.9350729870811,
11.2879605322915));
#165226=CARTESIAN_POINT('Ctrl Pts',(-16.6176515119966,-18.8621555742337,
11.2835839850319));
#165227=CARTESIAN_POINT('Ctrl Pts',(-16.6232479369201,-18.7894739153122,
11.2792074377722));
#165228=CARTESIAN_POINT('Ctrl Pts',(-16.6288408126722,-18.7168383500425,
11.2748336660552));
#165229=CARTESIAN_POINT('Ctrl Pts',(-16.6381914295876,-18.644438721819,
11.2704598943383));
#165230=CARTESIAN_POINT('Ctrl Pts',(-16.6512581694981,-18.5726908022763,
11.2660861226213));
#165231=CARTESIAN_POINT('Ctrl Pts',(-16.6643209331559,-18.5009647158666,
11.2617136818578));
#165232=CARTESIAN_POINT('Ctrl Pts',(-16.6810974883882,-18.4298904187035,
11.2573412410942));
#165233=CARTESIAN_POINT('Ctrl Pts',(-16.7014947532381,-18.3598755013638,
11.2529688003307));
#165234=CARTESIAN_POINT('Ctrl Pts',(-16.7218925396482,-18.2898587937348,
11.2485962477633));
#165235=CARTESIAN_POINT('Ctrl Pts',(-16.7459110826478,-18.2209019822761,
11.244223695196));
#165236=CARTESIAN_POINT('Ctrl Pts',(-16.7734073411525,-18.1533978299095,
11.2398511426286));
#165237=CARTESIAN_POINT('Ctrl Pts',(-16.8009321363114,-18.0858236191875,
11.2354740520613));
#165238=CARTESIAN_POINT('Ctrl Pts',(-16.8319416708366,-18.0197055253259,
11.231096961494));
#165239=CARTESIAN_POINT('Ctrl Pts',(-16.8662449207626,-17.9554158520311,
11.2267198709266));
#165240=CARTESIAN_POINT('Ctrl Pts',(-16.9005669049666,-17.8910910677596,
11.2223403898677));
#165241=CARTESIAN_POINT('Ctrl Pts',(-16.9381859370549,-17.8285971057583,
11.2179609088088));
#165242=CARTESIAN_POINT('Ctrl Pts',(-16.9788666145897,-17.7682788337543,
11.2135814277498));
#165243=CARTESIAN_POINT('Ctrl Pts',(-17.0196193983524,-17.7078536480181,
11.2091941840901));
#165244=CARTESIAN_POINT('Ctrl Pts',(-17.0634443742615,-17.6496122391292,
11.2048069404304));
#165245=CARTESIAN_POINT('Ctrl Pts',(-17.1100650454663,-17.5938673616161,
11.2004196967707));
#165246=CARTESIAN_POINT('Ctrl Pts',(-17.1417626095283,-17.5559662164709,
11.1974367938359));
#165247=CARTESIAN_POINT('Ctrl Pts',(-17.1747517071182,-17.5192184270681,
11.1944538909011));
#165248=CARTESIAN_POINT('Ctrl Pts',(-17.2089361619794,-17.4837121229262,
11.1914709879662));
#165249=CARTESIAN_POINT('Ctrl Pts',(-17.2592256059869,-17.4314780796657,
11.1870827790353));
#165250=CARTESIAN_POINT('Ctrl Pts',(-17.3122998738986,-17.3817287153967,
11.1826945701044));
#165251=CARTESIAN_POINT('Ctrl Pts',(-17.3678836195122,-17.3347755149755,
11.1783063611735));
#165252=CARTESIAN_POINT('Ctrl Pts',(-17.4233848696313,-17.2878920008886,
11.1739246650723));
#165253=CARTESIAN_POINT('Ctrl Pts',(-17.4813878383958,-17.2437967211,11.169542968971));
#165254=CARTESIAN_POINT('Ctrl Pts',(-17.5415797744863,-17.2027650227069,
11.1651612728697));
#165255=CARTESIAN_POINT('Ctrl Pts',(-17.6017009802615,-17.1617815398248,
11.1607847256101));
#165256=CARTESIAN_POINT('Ctrl Pts',(-17.6640056470484,-17.1238547573655,
11.1564081783505));
#165257=CARTESIAN_POINT('Ctrl Pts',(-17.7281486587459,-17.0892192616152,
11.1520316310908));
#165258=CARTESIAN_POINT('Ctrl Pts',(-17.7922509918777,-17.0546057311929,
11.1476578593739));
#165259=CARTESIAN_POINT('Ctrl Pts',(-17.858188933312,-17.0232795746617,
11.1432840876569));
#165260=CARTESIAN_POINT('Ctrl Pts',(-17.9255903577762,-16.9954308470285,
11.1389103159399));
#165261=CARTESIAN_POINT('Ctrl Pts',(-17.9929712717606,-16.9675905938567,
11.1345378751764));
#165262=CARTESIAN_POINT('Ctrl Pts',(-18.0618143390781,-16.943225852836,
11.1301654344128));
#165263=CARTESIAN_POINT('Ctrl Pts',(-18.1317264570585,-16.9224789778195,
11.1257929936492));
#165264=CARTESIAN_POINT('Ctrl Pts',(-18.2016403626994,-16.9017315723031,
11.1214204410819));
#165265=CARTESIAN_POINT('Ctrl Pts',(-18.2726229102619,-16.8846023517757,
11.1170478885146));
#165266=CARTESIAN_POINT('Ctrl Pts',(-18.3442664228592,-16.8711836364424,
11.1126753359472));
#165267=CARTESIAN_POINT('Ctrl Pts',(-18.4159842897962,-16.8577509946602,
11.1082982453799));
#165268=CARTESIAN_POINT('Ctrl Pts',(-18.4883640162148,-16.8480366356522,
11.1039211548126));
#165269=CARTESIAN_POINT('Ctrl Pts',(-18.5609891559668,-16.8420814594286,
11.0995440642452));
#165270=CARTESIAN_POINT('Ctrl Pts',(-18.633653959003,-16.8361230308623,
11.0951645831863));
#165271=CARTESIAN_POINT('Ctrl Pts',(-18.7065639597304,-16.833927887168,
11.0907851021273));
#165272=CARTESIAN_POINT('Ctrl Pts',(-18.7793017600918,-16.8354847625088,
11.0864056210684));
#165273=CARTESIAN_POINT('Ctrl Pts',(-18.8521684877161,-16.8370443974006,
11.0820183774087));
#165274=CARTESIAN_POINT('Ctrl Pts',(-18.9248619239421,-16.8423692966916,
11.077631133749));
#165275=CARTESIAN_POINT('Ctrl Pts',(-18.9969694292046,-16.851396258381,
11.0732438900892));
#165276=CARTESIAN_POINT('Ctrl Pts',(-19.0459955845204,-16.8575337224938,
11.0702609871544));
#165277=CARTESIAN_POINT('Ctrl Pts',(-19.094751032782,-16.8653814515023,
11.0672780842196));
#165278=CARTESIAN_POINT('Ctrl Pts',(-19.1431096126278,-16.8749062792316,
11.0642951812848));
#165279=CARTESIAN_POINT('Ctrl Pts',(-19.2142508990197,-16.8889184462449,
11.0599069723539));
#165280=CARTESIAN_POINT('Ctrl Pts',(-19.2848103359496,-16.9066171190662,
11.055518763423));
#165281=CARTESIAN_POINT('Ctrl Pts',(-19.3543769742702,-16.9279393759585,
11.0511305544921));
#165282=CARTESIAN_POINT('Ctrl Pts',(-19.4238403641655,-16.9492299870864,
11.0467488583909));
#165283=CARTESIAN_POINT('Ctrl Pts',(-19.4923134231175,-16.9741333660322,
11.0423671622896));
#165284=CARTESIAN_POINT('Ctrl Pts',(-19.5593953414347,-17.0025355785914,
11.0379854661883));
#165285=CARTESIAN_POINT('Ctrl Pts',(-19.6263984331591,-17.0309044162905,
11.0336089189286));
#165286=CARTESIAN_POINT('Ctrl Pts',(-19.6920131895943,-17.0627637331242,
11.029232371669));
#165287=CARTESIAN_POINT('Ctrl Pts',(-19.7558555559977,-17.0979503181747,
11.0248558244094));
#165288=CARTESIAN_POINT('Ctrl Pts',(-19.8196574345001,-17.1331145884042,
11.0204820526924));
#165289=CARTESIAN_POINT('Ctrl Pts',(-19.8816887317574,-17.1716017078621,
11.0161082809754));
#165290=CARTESIAN_POINT('Ctrl Pts',(-19.9415882172335,-17.2132016512548,
11.0117345092584));
#165291=CARTESIAN_POINT('Ctrl Pts',(-20.001469475095,-17.2547889356452,
11.0073620684949));
#165292=CARTESIAN_POINT('Ctrl Pts',(-20.0592198131165,-17.299486888407,
11.0029896277313));
#165293=CARTESIAN_POINT('Ctrl Pts',(-20.1145067552159,-17.3470420258451,
10.9986171869678));
#165294=CARTESIAN_POINT('Ctrl Pts',(-20.1697951110086,-17.3945983792735,
10.9942446344004));
#165295=CARTESIAN_POINT('Ctrl Pts',(-20.2226195814196,-17.4450117463521,
10.989872081833));
#165296=CARTESIAN_POINT('Ctrl Pts',(-20.2726818719996,-17.4979893065112,
10.9854995292657));
#165297=CARTESIAN_POINT('Ctrl Pts',(-20.3227961191128,-17.5510218487802,
10.9811224386983));
#165298=CARTESIAN_POINT('Ctrl Pts',(-20.3701421308281,-17.6066235460745,
10.976745348131));
#165299=CARTESIAN_POINT('Ctrl Pts',(-20.4144601023081,-17.6644663714874,
10.9723682575637));
#165300=CARTESIAN_POINT('Ctrl Pts',(-20.4588022774772,-17.7223407870142,
10.9679887765047));
#165301=CARTESIAN_POINT('Ctrl Pts',(-20.5001128464812,-17.7824583697207,
10.9636092954458));
#165302=CARTESIAN_POINT('Ctrl Pts',(-20.5381753524546,-17.8444620559118,
10.9592298143869));
#165303=CARTESIAN_POINT('Ctrl Pts',(-20.5763053239643,-17.9065756432203,
10.9548425707271));
#165304=CARTESIAN_POINT('Ctrl Pts',(-20.6111755046332,-17.9705815860921,
10.9504553270674));
#165305=CARTESIAN_POINT('Ctrl Pts',(-20.6426156833716,-18.0360987099104,
10.9460680834077));
#165306=CARTESIAN_POINT('Ctrl Pts',(-20.6639919753451,-18.0806440408914,
10.9430851804729));
#165307=CARTESIAN_POINT('Ctrl Pts',(-20.6837836766027,-18.1258874840305,
10.9401022775381));
#165308=CARTESIAN_POINT('Ctrl Pts',(-20.7019503858964,-18.1717050053665,
10.9371193746033));
#165309=CARTESIAN_POINT('Ctrl Pts',(-20.7090721959102,-18.1896666338036,
10.9359500011275));
#165310=CARTESIAN_POINT('Ctrl Pts',(-20.7159498696698,-18.207730262489,
10.9347806276517));
#165311=CARTESIAN_POINT('Ctrl Pts',(-20.7225805737622,-18.2258896078036,
10.9336112541758));
#165312=CARTESIAN_POINT('Ctrl Pts',(-20.7219729293147,-18.2261210096953,
11.7337477406533));
#165313=CARTESIAN_POINT('Ctrl Pts',(-20.7875397462696,-18.4003672652382,
11.7225565653328));
#165314=CARTESIAN_POINT('Ctrl Pts',(-20.8444160987049,-18.6428894722044,
11.7076594114559));
#165315=CARTESIAN_POINT('Ctrl Pts',(-20.8542040030872,-18.8895339278279,
11.692762257579));
#165316=CARTESIAN_POINT('Ctrl Pts',(-20.8538228987003,-18.9509225630713,
11.6890562790225));
#165317=CARTESIAN_POINT('Origin',(-18.734,-18.952,0.));
#165318=CARTESIAN_POINT('',(-20.7225806094135,-18.2258897054408,12.7565302021861));
#165319=CARTESIAN_POINT('',(-20.722580563326,-18.2258895792221,12.5316746529861));
#165320=CARTESIAN_POINT('',(-20.7225805737622,-18.2258896078036,0.));
#165321=CARTESIAN_POINT('',(-20.850999902,-18.9513558477209,12.7090270570735));
#165322=CARTESIAN_POINT('Ctrl Pts',(-20.7225806094134,-18.2258897054408,
12.7565302021861));
#165323=CARTESIAN_POINT('Ctrl Pts',(-20.7842551302578,-18.3947962161526,
12.7448317476997));
#165324=CARTESIAN_POINT('Ctrl Pts',(-20.8241856933643,-18.5709417764268,
12.7326638034165));
#165325=CARTESIAN_POINT('Ctrl Pts',(-20.8438467731545,-18.7761570303496,
12.7196401132585));
#165326=CARTESIAN_POINT('Ctrl Pts',(-20.8458598049362,-18.8022586722148,
12.7180061119518));
#165327=CARTESIAN_POINT('Ctrl Pts',(-20.8477953012514,-18.8353508994641,
12.7159685240739));
#165328=CARTESIAN_POINT('Ctrl Pts',(-20.8481679331215,-18.8423116144406,
12.7155418364321));
#165329=CARTESIAN_POINT('Ctrl Pts',(-20.8487046761409,-18.8533599189729,
12.7148677392846));
#165330=CARTESIAN_POINT('Ctrl Pts',(-20.848891328097,-18.8574462910722,
12.714619099899));
#165331=CARTESIAN_POINT('Ctrl Pts',(-20.8492163337029,-18.8650447524985,
12.7141580697768));
#165332=CARTESIAN_POINT('Ctrl Pts',(-20.8493577838477,-18.8685566062754,
12.7139455132782));
#165333=CARTESIAN_POINT('Ctrl Pts',(-20.849621826542,-18.8755448703287,
12.7135235698769));
#165334=CARTESIAN_POINT('Ctrl Pts',(-20.8497445963114,-18.8790212128661,
12.7133141745303));
#165335=CARTESIAN_POINT('Ctrl Pts',(-20.8500062524825,-18.8869868323075,
12.712835488951));
#165336=CARTESIAN_POINT('Ctrl Pts',(-20.8501394223501,-18.891476297842,
12.7125665130544));
#165337=CARTESIAN_POINT('Ctrl Pts',(-20.8504746949752,-18.9041387170784,
12.7118100836978));
#165338=CARTESIAN_POINT('Ctrl Pts',(-20.850643746382,-18.9123125648082,
12.7113243893412));
#165339=CARTESIAN_POINT('Ctrl Pts',(-20.8509186141009,-18.9307759480992,
12.7102327380662));
#165340=CARTESIAN_POINT('Ctrl Pts',(-20.8509967709633,-18.9410657275654,
12.7096281764806));
#165341=CARTESIAN_POINT('Ctrl Pts',(-20.850999902,-18.9513558477209,12.7090270570735));
#165342=CARTESIAN_POINT('Ctrl Pts',(-20.8509999014168,-18.9513539340914,
12.7090271688623));
#165343=CARTESIAN_POINT('Ctrl Pts',(-20.8510612391395,-19.1523426431075,
12.6972859745878));
#165344=CARTESIAN_POINT('Ctrl Pts',(-20.8225007095598,-19.3523598025333,
12.686841735807));
#165345=CARTESIAN_POINT('Ctrl Pts',(-20.7414616181698,-19.6298921790064,
12.6708792396687));
#165346=CARTESIAN_POINT('Ctrl Pts',(-20.7115396446143,-19.7127722168093,
12.6659227412855));
#165347=CARTESIAN_POINT('Ctrl Pts',(-20.6684009395749,-19.8123499657298,
12.6595977270179));
#165348=CARTESIAN_POINT('Ctrl Pts',(-20.6599812421858,-19.8310365577107,
12.6583943619046));
#165349=CARTESIAN_POINT('Ctrl Pts',(-20.6475367860491,-19.8576182423343,
12.6566576870789));
#165350=CARTESIAN_POINT('Ctrl Pts',(-20.6437315486392,-19.8656152586905,
12.6561319492906));
#165351=CARTESIAN_POINT('Ctrl Pts',(-20.6370470758175,-19.8794389817198,
12.6552173772543));
#165352=CARTESIAN_POINT('Ctrl Pts',(-20.6341909602551,-19.8852767814013,
12.6548293512496));
#165353=CARTESIAN_POINT('Ctrl Pts',(-20.6286470864462,-19.8964773158425,
12.6540813686199));
#165354=CARTESIAN_POINT('Ctrl Pts',(-20.6259633239602,-19.9018419668335,
12.6537215547101));
#165355=CARTESIAN_POINT('Ctrl Pts',(-20.6188715792426,-19.9158685537708,
12.6527766469076));
#165356=CARTESIAN_POINT('Ctrl Pts',(-20.6144267212606,-19.9245115938773,
12.6521902601561));
#165357=CARTESIAN_POINT('Ctrl Pts',(-20.59878635266,-19.9544162053493,12.6501467568832));
#165358=CARTESIAN_POINT('Ctrl Pts',(-20.5872888085937,-19.9755169305429,
12.6486789921802));
#165359=CARTESIAN_POINT('Ctrl Pts',(-20.5034337899779,-20.1233636272135,
12.6382063136606));
#165360=CARTESIAN_POINT('Ctrl Pts',(-20.4185110369099,-20.2425027481767,
12.6287338943812));
#165361=CARTESIAN_POINT('Ctrl Pts',(-20.2315227060658,-20.4546135714325,
12.6100722358669));
#165362=CARTESIAN_POINT('Ctrl Pts',(-20.1312642119496,-20.5482706947719,
12.6009551399618));
#165363=CARTESIAN_POINT('Ctrl Pts',(-20.0125804401966,-20.6393299707194,
12.5915872719988));
#165364=CARTESIAN_POINT('Ctrl Pts',(-20.0024322136796,-20.6469720081385,
12.5907968161615));
#165365=CARTESIAN_POINT('Ctrl Pts',(-19.9867977241588,-20.6585263685953,
12.5895958516412));
#165366=CARTESIAN_POINT('Ctrl Pts',(-19.9813607340329,-20.6625044829779,
12.5891812795801));
#165367=CARTESIAN_POINT('Ctrl Pts',(-19.9723708089455,-20.669016535008,
12.5885009640533));
#165368=CARTESIAN_POINT('Ctrl Pts',(-19.9688289097377,-20.6715655283782,
12.5882342412073));
#165369=CARTESIAN_POINT('Ctrl Pts',(-19.961967221705,-20.6764715359513,
12.5877200918417));
#165370=CARTESIAN_POINT('Ctrl Pts',(-19.9586484683809,-20.6788299584572,
12.5874725710454));
#165371=CARTESIAN_POINT('Ctrl Pts',(-19.9553132060688,-20.6811856617561,
12.5872249921127));
#165372=CARTESIAN_POINT('Ctrl Pts',(-19.955303512298,-20.6811925083661,
12.587224272547));
#165373=CARTESIAN_POINT('Ctrl Pts',(-19.9552840912867,-20.6812062249807,
12.587222830951));
#165374=CARTESIAN_POINT('Ctrl Pts',(-19.9552743627046,-20.6812130959319,
12.5872221088213));
#165375=CARTESIAN_POINT('Ctrl Pts',(-19.9552548707649,-20.6812268621485,
12.5872206620004));
#165376=CARTESIAN_POINT('Ctrl Pts',(-19.9552451082536,-20.6812337568153,
12.5872199373722));
#165377=CARTESIAN_POINT('Ctrl Pts',(-19.9552249152373,-20.6812480176559,
12.5872184385544));
#165378=CARTESIAN_POINT('Ctrl Pts',(-19.9552144846205,-20.681255383891,
12.587217664358));
#165379=CARTESIAN_POINT('Ctrl Pts',(-19.9551934551847,-20.6812702348628,
12.5872161035036));
#165380=CARTESIAN_POINT('Ctrl Pts',(-19.9551828565233,-20.6812777194835,
12.5872153168578));
#165381=CARTESIAN_POINT('Ctrl Pts',(-19.9551614878196,-20.6812928094571,
12.58721373087));
#165382=CARTESIAN_POINT('Ctrl Pts',(-19.9551507172095,-20.6813004152062,
12.5872129314862));
#165383=CARTESIAN_POINT('Ctrl Pts',(-19.955129000285,-20.6813157504755,
12.5872113197028));
#165384=CARTESIAN_POINT('Ctrl Pts',(-19.9551180547392,-20.6813234794478,
12.5872105073606));
#165385=CARTESIAN_POINT('Ctrl Pts',(-19.9550959841774,-20.6813390638077,
12.587208869382));
#165386=CARTESIAN_POINT('Ctrl Pts',(-19.9550848592426,-20.6813469191327,
12.5872080437521));
#165387=CARTESIAN_POINT('Ctrl Pts',(-19.9550624268276,-20.681362758354,
12.587206378971));
#165388=CARTESIAN_POINT('Ctrl Pts',(-19.9550511185571,-20.6813707428027,
12.5872055397617));
#165389=CARTESIAN_POINT('Ctrl Pts',(-19.955028315119,-20.6813868433279,
12.5872038475003));
#165390=CARTESIAN_POINT('Ctrl Pts',(-19.95501682013,-20.6813949592727,12.5872029944619));
#165391=CARTESIAN_POINT('Ctrl Pts',(-19.9549936383322,-20.6814113262486,
12.5872012741783));
#165392=CARTESIAN_POINT('Ctrl Pts',(-19.9549819524341,-20.6814195766311,
12.5872004070012));
#165393=CARTESIAN_POINT('Ctrl Pts',(-19.9549583850607,-20.681436215118,
12.5871986581629));
#165394=CARTESIAN_POINT('Ctrl Pts',(-19.954946503419,-20.6814446033338,
12.5871977764898));
#165395=CARTESIAN_POINT('Ctrl Pts',(-19.9549225406218,-20.6814615202485,
12.5871959983688));
#165396=CARTESIAN_POINT('Ctrl Pts',(-19.9549104592121,-20.6814700491206,
12.5871951019025));
#165397=CARTESIAN_POINT('Ctrl Pts',(-19.9548860920947,-20.6814872507064,
12.5871932938417));
#165398=CARTESIAN_POINT('Ctrl Pts',(-19.9548738066287,-20.681495923243,
12.5871923822657));
#165399=CARTESIAN_POINT('Ctrl Pts',(-19.954849027269,-20.6815134150535,
12.5871905436804));
#165400=CARTESIAN_POINT('Ctrl Pts',(-19.95483653264,-20.6815222348399,12.5871896166172));
#165401=CARTESIAN_POINT('Ctrl Pts',(-19.9548113297571,-20.6815400247982,
12.5871877466738));
#165402=CARTESIAN_POINT('Ctrl Pts',(-19.9547986219221,-20.6815489946674,
12.5871868038252));
#165403=CARTESIAN_POINT('Ctrl Pts',(-19.9547729872369,-20.6815670885754,
12.5871849019127));
#165404=CARTESIAN_POINT('Ctrl Pts',(-19.9547600609693,-20.6815762121955,
12.5871839428926));
#165405=CARTESIAN_POINT('Ctrl Pts',(-19.9547339853479,-20.6815946164566,
12.5871820083369));
#165406=CARTESIAN_POINT('Ctrl Pts',(-19.9547208350335,-20.681603897768,
12.5871810327307));
#165407=CARTESIAN_POINT('Ctrl Pts',(-19.951870269543,-20.6836157390526,
12.5869695566085));
#165408=CARTESIAN_POINT('Ctrl Pts',(-19.9490279715372,-20.6856112856507,
12.5867595473815));
#165409=CARTESIAN_POINT('Ctrl Pts',(-19.9424087574977,-20.6902342887562,
12.5862724356391));
#165410=CARTESIAN_POINT('Ctrl Pts',(-19.9386281822933,-20.6928564303659,
12.5859956971577));
#165411=CARTESIAN_POINT('Ctrl Pts',(-19.9269336200905,-20.7009112389434,
12.5851441000283));
#165412=CARTESIAN_POINT('Ctrl Pts',(-19.9189910813986,-20.7063025076916,
12.5845719811846));
#165413=CARTESIAN_POINT('Ctrl Pts',(-19.8165018853544,-20.774856890051,
12.5772656694361));
#165414=CARTESIAN_POINT('Ctrl Pts',(-19.7170380195521,-20.8303666186062,
12.5709986813682));
#165415=CARTESIAN_POINT('Ctrl Pts',(-19.5099096779756,-20.9249784783313,
12.5585882098859));
#165416=CARTESIAN_POINT('Ctrl Pts',(-19.4025841859592,-20.9638832721718,
12.5524608812122));
#165417=CARTESIAN_POINT('Ctrl Pts',(-19.2395015422013,-21.0085002744369,
12.5430595920196));
#165418=CARTESIAN_POINT('Ctrl Pts',(-19.1858089059056,-21.0209594619883,
12.5399525323494));
#165419=CARTESIAN_POINT('Ctrl Pts',(-19.0980009687977,-21.0377538317525,
12.5348092099037));
#165420=CARTESIAN_POINT('Ctrl Pts',(-19.0641577550619,-21.0433778740814,
12.5328123209596));
#165421=CARTESIAN_POINT('Ctrl Pts',(-19.0194920268192,-21.0496892347899,
12.5301519287645));
#165422=CARTESIAN_POINT('Ctrl Pts',(-19.0087785947121,-21.0511194678868,
12.5295119480867));
#165423=CARTESIAN_POINT('Ctrl Pts',(-18.9912106199051,-21.053327980227,
12.5284592727455));
#165424=CARTESIAN_POINT('Ctrl Pts',(-18.9843623105729,-21.0541549170291,
12.5280481191861));
#165425=CARTESIAN_POINT('Ctrl Pts',(-18.97109613001,-21.0556910696015,12.527250053999));
#165426=CARTESIAN_POINT('Ctrl Pts',(-18.9646788079533,-21.0564044234214,
12.5268632777076));
#165427=CARTESIAN_POINT('Ctrl Pts',(-18.9498509881428,-21.0579840543809,
12.5259678812714));
#165428=CARTESIAN_POINT('Ctrl Pts',(-18.9414384057287,-21.0588293217481,
12.5254586049149));
#165429=CARTESIAN_POINT('Ctrl Pts',(-18.9187935851571,-21.0609676520636,
12.524084226225));
#165430=CARTESIAN_POINT('Ctrl Pts',(-18.9045531343256,-21.0621670169011,
12.5232161953583));
#165431=CARTESIAN_POINT('Ctrl Pts',(-18.7737085188745,-21.0718539475933,
12.5152049561027));
#165432=CARTESIAN_POINT('Ctrl Pts',(-18.6566197340488,-21.0708114595135,
12.5077596230227));
#165433=CARTESIAN_POINT('Ctrl Pts',(-18.3779984381195,-21.0452017959662,
12.489483089061));
#165434=CARTESIAN_POINT('Ctrl Pts',(-18.2180333724804,-21.0116138990888,
12.478511338309));
#165435=CARTESIAN_POINT('Ctrl Pts',(-18.0328851287785,-20.9497910157762,
12.4661107371694));
#165436=CARTESIAN_POINT('Ctrl Pts',(-18.0025026881001,-20.9388676230098,
12.464087885336));
#165437=CARTESIAN_POINT('Ctrl Pts',(-17.9656398434069,-20.9246540132009,
12.461658499323));
#165438=CARTESIAN_POINT('Ctrl Pts',(-17.9589127810326,-20.922020556364,
12.4612161939852));
#165439=CARTESIAN_POINT('Ctrl Pts',(-17.9483832486745,-20.9178362549301,
12.4605256450925));
#165440=CARTESIAN_POINT('Ctrl Pts',(-17.9445716598825,-20.9163087225898,
12.4602760383103));
#165441=CARTESIAN_POINT('Ctrl Pts',(-17.9374523788119,-20.9134315305656,
12.4598105398065));
#165442=CARTESIAN_POINT('Ctrl Pts',(-17.9341436950112,-20.9120846036624,
12.459594493906));
#165443=CARTESIAN_POINT('Ctrl Pts',(-17.9265947240782,-20.9089892071009,
12.4591022275286));
#165444=CARTESIAN_POINT('Ctrl Pts',(-17.9223567076918,-20.9072353319371,
12.4588263379766));
#165445=CARTESIAN_POINT('Ctrl Pts',(-17.909334266407,-20.9017964437046,
12.4579799438881));
#165446=CARTESIAN_POINT('Ctrl Pts',(-17.9005688474748,-20.8980658431091,
12.4574121309444));
#165447=CARTESIAN_POINT('Ctrl Pts',(-17.7831681757499,-20.8471608908244,
12.4498287387907));
#165448=CARTESIAN_POINT('Ctrl Pts',(-17.6786363507224,-20.7910028952994,
12.4433207111902));
#165449=CARTESIAN_POINT('Ctrl Pts',(-17.4876881413444,-20.6667456969204,
12.4309173567455));
#165450=CARTESIAN_POINT('Ctrl Pts',(-17.400796255379,-20.6000937308301,
12.425029338071));
#165451=CARTESIAN_POINT('Ctrl Pts',(-17.2784448505951,-20.4902084161776,
12.4158851680527));
#165452=CARTESIAN_POINT('Ctrl Pts',(-17.2389006551485,-20.451801062896,
12.4127777468981));
#165453=CARTESIAN_POINT('Ctrl Pts',(-17.177243440619,-20.3870522548753,
12.4076338794243));
#165454=CARTESIAN_POINT('Ctrl Pts',(-17.1541937093006,-20.3616374876838,
12.4056368178807));
#165455=CARTESIAN_POINT('Ctrl Pts',(-17.1247079047787,-20.3274943776321,
12.4029762283239));
#165456=CARTESIAN_POINT('Ctrl Pts',(-17.1177060961681,-20.319259975468,
12.4023362273389));
#165457=CARTESIAN_POINT('Ctrl Pts',(-17.1063395962732,-20.3056831958284,
12.4012835271038));
#165458=CARTESIAN_POINT('Ctrl Pts',(-17.1019373622001,-20.3003724000048,
12.4008723691006));
#165459=CARTESIAN_POINT('Ctrl Pts',(-17.0934649359626,-20.2900491001653,
12.4000743013691));
#165460=CARTESIAN_POINT('Ctrl Pts',(-17.0893915608178,-20.2850392984183,
12.3996875270095));
#165461=CARTESIAN_POINT('Ctrl Pts',(-17.0800374552795,-20.2734266471797,
12.3987921439049));
#165462=CARTESIAN_POINT('Ctrl Pts',(-17.074773260848,-20.2668106738457,
12.3982828790098));
#165463=CARTESIAN_POINT('Ctrl Pts',(-17.0607185547714,-20.2489280678248,
12.3969085513041));
#165464=CARTESIAN_POINT('Ctrl Pts',(-17.0520023744138,-20.2376038191693,
12.3960405602985));
#165465=CARTESIAN_POINT('Ctrl Pts',(-16.973063263971,-20.1328674174481,
12.3880323656874));
#165466=CARTESIAN_POINT('Ctrl Pts',(-16.9105846302004,-20.0338939991308,
12.3805903036596));
#165467=CARTESIAN_POINT('Ctrl Pts',(-16.7813812202447,-19.7859431800545,
12.3623272407322));
#165468=CARTESIAN_POINT('Ctrl Pts',(-16.7230648940813,-19.6334113338907,
12.3513660787218));
#165469=CARTESIAN_POINT('Ctrl Pts',(-16.6747700494817,-19.44425465347,12.3389616388116));
#165470=CARTESIAN_POINT('Ctrl Pts',(-16.6674640221976,-19.4126212683758,
12.336927276411));
#165471=CARTESIAN_POINT('Ctrl Pts',(-16.6594221529178,-19.3737441414188,
12.3344860207624));
#165472=CARTESIAN_POINT('Ctrl Pts',(-16.6579926439531,-19.3666502448422,
12.3340429512458));
#165473=CARTESIAN_POINT('Ctrl Pts',(-16.6558084900638,-19.35551695315,12.3333514763866));
#165474=CARTESIAN_POINT('Ctrl Pts',(-16.6550291990208,-19.3514825312694,
12.3331017019038));
#165475=CARTESIAN_POINT('Ctrl Pts',(-16.6535944205046,-19.3439367090584,
12.3326360583764));
#165476=CARTESIAN_POINT('Ctrl Pts',(-16.6529360810056,-19.3404259574133,
12.3324200341421));
#165477=CARTESIAN_POINT('Ctrl Pts',(-16.6514534371299,-19.3324074291078,
12.3319280343614));
#165478=CARTESIAN_POINT('Ctrl Pts',(-16.6506348827829,-19.3278986404755,
12.3316523883594));
#165479=CARTESIAN_POINT('Ctrl Pts',(-16.648163490553,-19.3140295587745,
12.3308074836315));
#165480=CARTESIAN_POINT('Ctrl Pts',(-16.6465590202981,-19.3046606151112,
12.3302409027775));
#165481=CARTESIAN_POINT('Ctrl Pts',(-16.6325556183956,-19.2194451203275,
12.3251228479428));
#165482=CARTESIAN_POINT('Ctrl Pts',(-16.6242309300783,-19.1429778656906,
12.3207831191346));
#165483=CARTESIAN_POINT('Ctrl Pts',(-16.6125055597645,-18.9259703485235,
12.3087614966779));
#165484=CARTESIAN_POINT('Ctrl Pts',(-16.6189032404143,-18.785314413875,
12.3012942278611));
#165485=CARTESIAN_POINT('Ctrl Pts',(-16.6481295180311,-18.585024370231,
12.2900977769894));
#165486=CARTESIAN_POINT('Ctrl Pts',(-16.6597603175682,-18.5241499605522,
12.2866218511884));
#165487=CARTESIAN_POINT('Ctrl Pts',(-16.6826474542289,-18.4275627398131,
12.2809257168568));
#165488=CARTESIAN_POINT('Ctrl Pts',(-16.6922104990834,-18.391484977906,
12.2787569445543));
#165489=CARTESIAN_POINT('Ctrl Pts',(-16.7058599115212,-18.3449901898627,
12.2759005606723));
#165490=CARTESIAN_POINT('Ctrl Pts',(-16.7090824974773,-18.3343251430565,
12.2752411258006));
#165491=CARTESIAN_POINT('Ctrl Pts',(-16.7144581452528,-18.3170289003503,
12.2741645814064));
#165492=CARTESIAN_POINT('Ctrl Pts',(-16.7165600712629,-18.3103819417936,
12.2737491523528));
#165493=CARTESIAN_POINT('Ctrl Pts',(-16.7206638549152,-18.2976240245678,
12.2729484469735));
#165494=CARTESIAN_POINT('Ctrl Pts',(-16.7226608024148,-18.2915115586397,
12.2725633361454));
#165495=CARTESIAN_POINT('Ctrl Pts',(-16.7272947159195,-18.2775435031022,
12.2716798478149));
#165496=CARTESIAN_POINT('Ctrl Pts',(-16.7299500056479,-18.2696941444976,
12.2711808690808));
#165497=CARTESIAN_POINT('Ctrl Pts',(-16.7371217747854,-18.2488965892592,
12.2698520341522));
#165498=CARTESIAN_POINT('Ctrl Pts',(-16.7417180434729,-18.235976505735,
12.269019543779));
#165499=CARTESIAN_POINT('Ctrl Pts',(-16.7773883480091,-18.1387106159658,
12.2626984910875));
#165500=CARTESIAN_POINT('Ctrl Pts',(-16.8136765303748,-18.0563868726964,
12.2570352034524));
#165501=CARTESIAN_POINT('Ctrl Pts',(-16.9387267606208,-17.8154953874751,
12.2395150988989));
#165502=CARTESIAN_POINT('Ctrl Pts',(-17.0427411391216,-17.6658100853745,
12.2272413147993));
#165503=CARTESIAN_POINT('Ctrl Pts',(-17.1919832629446,-17.5009513709122,
12.2130076623627));
#165504=CARTESIAN_POINT('Ctrl Pts',(-17.2202717120241,-17.4714646512346,
12.2104329629849));
#165505=CARTESIAN_POINT('Ctrl Pts',(-17.2549130830892,-17.4373875924457,
12.2074417507908));
#165506=CARTESIAN_POINT('Ctrl Pts',(-17.2604581246782,-17.4319923688335,
12.2069676864878));
#165507=CARTESIAN_POINT('Ctrl Pts',(-17.2690718494115,-17.423702808949,
12.206238734394));
#165508=CARTESIAN_POINT('Ctrl Pts',(-17.2721197482174,-17.4207871079681,
12.2059822286026));
#165509=CARTESIAN_POINT('Ctrl Pts',(-17.277757044485,-17.415426494905,12.205510465449));
#165510=CARTESIAN_POINT('Ctrl Pts',(-17.2803438779467,-17.4129790250947,
12.2052950130511));
#165511=CARTESIAN_POINT('Ctrl Pts',(-17.2861664713532,-17.4074978971642,
12.204812356883));
#165512=CARTESIAN_POINT('Ctrl Pts',(-17.2894055859539,-17.4044678833482,
12.2045454330141));
#165513=CARTESIAN_POINT('Ctrl Pts',(-17.2977011590739,-17.3967565718223,
12.203865768786));
#165514=CARTESIAN_POINT('Ctrl Pts',(-17.3027710387789,-17.3920896997441,
12.20345410578));
#165515=CARTESIAN_POINT('Ctrl Pts',(-17.3322075198944,-17.3652574669085,
12.2010846896061));
#165516=CARTESIAN_POINT('Ctrl Pts',(-17.3570674655592,-17.3436371402183,
12.1991653423855));
#165517=CARTESIAN_POINT('Ctrl Pts',(-17.396620213705,-17.310828303685,12.1962180080169));
#165518=CARTESIAN_POINT('Ctrl Pts',(-17.4109707383532,-17.299237815461,
12.195169621709));
#165519=CARTESIAN_POINT('Ctrl Pts',(-17.4266368427481,-17.2869195894767,
12.1940453348911));
#165520=CARTESIAN_POINT('Ctrl Pts',(-17.4278033640929,-17.2860043376977,
12.1939617384597));
#165521=CARTESIAN_POINT('Ctrl Pts',(-17.4470154902811,-17.2709631000707,
12.1925868894683));
#165522=CARTESIAN_POINT('Ctrl Pts',(-17.4652887999205,-17.2571294649188,
12.1913074953054));
#165523=CARTESIAN_POINT('Ctrl Pts',(-17.5206421305975,-17.2166217158637,
12.187504149114));
#165524=CARTESIAN_POINT('Ctrl Pts',(-17.5583650388148,-17.1908475981306,
12.185006662383));
#165525=CARTESIAN_POINT('Ctrl Pts',(-17.689129584563,-17.1075780833495,
12.1765663795622));
#165526=CARTESIAN_POINT('Ctrl Pts',(-17.7857773494415,-17.0560782418667,
12.1706782853511));
#165527=CARTESIAN_POINT('Ctrl Pts',(-17.9364618904714,-16.990200037325,
12.1615339397195));
#165528=CARTESIAN_POINT('Ctrl Pts',(-17.9877968473332,-16.9701053662525,
12.1584264179042));
#165529=CARTESIAN_POINT('Ctrl Pts',(-18.0722657434502,-16.9407879796317,
12.1532823986603));
#165530=CARTESIAN_POINT('Ctrl Pts',(-18.1049439412612,-16.9303288359542,
12.1512852890553));
#165531=CARTESIAN_POINT('Ctrl Pts',(-18.1482320592959,-16.917624972535,
12.1486246445422));
#165532=CARTESIAN_POINT('Ctrl Pts',(-18.1586265830274,-16.9146607407668,
12.1479846379027));
#165533=CARTESIAN_POINT('Ctrl Pts',(-18.1756912096942,-16.909935388023,
12.1469319307361));
#165534=CARTESIAN_POINT('Ctrl Pts',(-18.1823481084893,-16.9081270162551,
12.1465207714955));
#165535=CARTESIAN_POINT('Ctrl Pts',(-18.1952528780968,-16.9046890247645,
12.1457227030556));
#165536=CARTESIAN_POINT('Ctrl Pts',(-18.2014996069073,-16.9030553885958,
12.1453359292337));
#165537=CARTESIAN_POINT('Ctrl Pts',(-18.2159429960573,-16.8993486845064,
12.1444405498408));
#165538=CARTESIAN_POINT('Ctrl Pts',(-18.2241447560392,-16.8972961017953,
12.1439312881368));
#165539=CARTESIAN_POINT('Ctrl Pts',(-18.2462414759635,-16.8919065979584,
12.142556974626));
#165540=CARTESIAN_POINT('Ctrl Pts',(-18.2601581055755,-16.8886611896549,
12.1416889947183));
#165541=CARTESIAN_POINT('Ctrl Pts',(-18.3881654620941,-16.8601727285179,
12.1336816449845));
#165542=CARTESIAN_POINT('Ctrl Pts',(-18.5041116239165,-16.8442793380637,
12.1262404905973));
#165543=CARTESIAN_POINT('Ctrl Pts',(-18.7832506382352,-16.8293266590199,
12.1079811353664));
#165544=CARTESIAN_POINT('Ctrl Pts',(-18.9461978858044,-16.8393855372662,
12.0970228792225));
#165545=CARTESIAN_POINT('Ctrl Pts',(-19.138386052334,-16.8737272155504,
12.0846173746019));
#165546=CARTESIAN_POINT('Ctrl Pts',(-19.1702544521889,-16.8801824000517,
12.0825798424081));
#165547=CARTESIAN_POINT('Ctrl Pts',(-19.2090240659695,-16.8889698135634,
12.0801353193325));
#165548=CARTESIAN_POINT('Ctrl Pts',(-19.2160765452415,-16.8906063885287,
12.079692040249));
#165549=CARTESIAN_POINT('Ctrl Pts',(-19.2271191030206,-16.8932286577184,
12.0790003114699));
#165550=CARTESIAN_POINT('Ctrl Pts',(-19.2311148655619,-16.8941898288071,
12.0787504910105));
#165551=CARTESIAN_POINT('Ctrl Pts',(-19.2385782161104,-16.896008126921,
12.0782848076529));
#165552=CARTESIAN_POINT('Ctrl Pts',(-19.2420463956531,-16.8968623845508,
12.0780687892881));
#165553=CARTESIAN_POINT('Ctrl Pts',(-19.2499580407104,-16.8988323768892,
12.0775768622755));
#165554=CARTESIAN_POINT('Ctrl Pts',(-19.2544000483055,-16.8999537580763,
12.0773012827949));
#165555=CARTESIAN_POINT('Ctrl Pts',(-19.2680411881867,-16.9034445952605,
12.0764567846013));
#165556=CARTESIAN_POINT('Ctrl Pts',(-19.2772281866383,-16.9058615927029,
12.0758905400213));
#165557=CARTESIAN_POINT('Ctrl Pts',(-19.3595540168945,-16.9281141682154,
12.0708363287185));
#165558=CARTESIAN_POINT('Ctrl Pts',(-19.4316033569615,-16.9518040498019,
12.0665541470102));
#165559=CARTESIAN_POINT('Ctrl Pts',(-19.5420547864612,-16.9948176796213,
12.0599933660978));
#165560=CARTESIAN_POINT('Ctrl Pts',(-19.5813978578913,-17.0115278332892,
12.0576573178351));
#165561=CARTESIAN_POINT('Ctrl Pts',(-19.7194907374371,-17.0751813713442,
12.0493788238817));
#165562=CARTESIAN_POINT('Ctrl Pts',(-19.8150774163368,-17.1285661812524,
12.0434921246998));
#165563=CARTESIAN_POINT('Ctrl Pts',(-19.9519739602529,-17.2195849877405,
12.0343510222341));
#165564=CARTESIAN_POINT('Ctrl Pts',(-19.9966274853965,-17.2518548499242,
12.0312453593004));
#165565=CARTESIAN_POINT('Ctrl Pts',(-20.0669593926149,-17.3069820037024,
12.0261041428463));
#165566=CARTESIAN_POINT('Ctrl Pts',(-20.0934296067029,-17.3287883999349,
12.0241079208864));
#165567=CARTESIAN_POINT('Ctrl Pts',(-20.1275293224879,-17.35829933128,12.0214482913757));
#165568=CARTESIAN_POINT('Ctrl Pts',(-20.1356467608099,-17.3654338509006,
12.020808389187));
#165569=CARTESIAN_POINT('Ctrl Pts',(-20.1488551365414,-17.3772233421804,
12.0197558100631));
#165570=CARTESIAN_POINT('Ctrl Pts',(-20.1539786417032,-17.3818416529578,
12.0193446736788));
#165571=CARTESIAN_POINT('Ctrl Pts',(-20.163854363553,-17.3908314659357,
12.018546618321));
#165572=CARTESIAN_POINT('Ctrl Pts',(-20.1686093357417,-17.3951998377782,
12.0181598345593));
#165573=CARTESIAN_POINT('Ctrl Pts',(-20.1795448203177,-17.4053388635151,
12.0172643865765));
#165574=CARTESIAN_POINT('Ctrl Pts',(-20.1857108612714,-17.4111249010105,
12.0167550659061));
#165575=CARTESIAN_POINT('Ctrl Pts',(-20.2022061742281,-17.4267905297658,
12.0153804900842));
#165576=CARTESIAN_POINT('Ctrl Pts',(-20.2124701887747,-17.4367379159664,
12.0145123050927));
#165577=CARTESIAN_POINT('Ctrl Pts',(-20.3058954048566,-17.5291340959966,
12.0064891405521));
#165578=CARTESIAN_POINT('Ctrl Pts',(-20.3821685976282,-17.6182327929685,
11.9990309919019));
#165579=CARTESIAN_POINT('Ctrl Pts',(-20.5463777626565,-17.8457806850625,
11.9806999008511));
#165580=CARTESIAN_POINT('Ctrl Pts',(-20.6263877623316,-17.9890342248282,
11.9696847637001));
#165581=CARTESIAN_POINT('Ctrl Pts',(-20.700887556571,-18.1684278677764,
11.9573529660037));
#165582=CARTESIAN_POINT('Ctrl Pts',(-20.7120470190104,-18.1970416219089,
11.9554289491706));
#165583=CARTESIAN_POINT('Ctrl Pts',(-20.7225805737639,-18.2258896078082,
11.9535388216361));
#165584=CARTESIAN_POINT('',(-20.8516473850063,-18.9538935158916,12.4890562790225));
#165585=CARTESIAN_POINT('Ctrl Pts',(-20.8516473850063,-18.9538935158916,
12.4890562790225));
#165586=CARTESIAN_POINT('Ctrl Pts',(-20.8529700926033,-19.0968822287437,
12.4804472042752));
#165587=CARTESIAN_POINT('Ctrl Pts',(-20.7745204165097,-19.942518370496,
12.4294461939675));
#165588=CARTESIAN_POINT('Ctrl Pts',(-19.6371491297831,-21.2866630700929,
12.336053248099));
#165589=CARTESIAN_POINT('Ctrl Pts',(-17.2597753208662,-20.9751143311526,
12.2088774414178));
#165590=CARTESIAN_POINT('Ctrl Pts',(-16.2349111543522,-18.8074837620172,
12.0817016347362));
#165591=CARTESIAN_POINT('Ctrl Pts',(-17.5028058927726,-16.7724378715414,
11.9545258280549));
#165592=CARTESIAN_POINT('Ctrl Pts',(-19.6892757572449,-16.7401229693189,
11.8385411966939));
#165593=CARTESIAN_POINT('Ctrl Pts',(-20.5391740295624,-17.7403261323705,
11.7649485008933));
#165594=CARTESIAN_POINT('Ctrl Pts',(-20.7219729293147,-18.2261210096953,
11.7337477406533));
#165595=CARTESIAN_POINT('Ctrl Pts',(-20.8509991358391,-18.9539128137851,
12.4894293403473));
#165596=CARTESIAN_POINT('Ctrl Pts',(-20.8511381828998,-18.8000230260387,
12.4977966149232));
#165597=CARTESIAN_POINT('Ctrl Pts',(-20.834498149614,-18.6465855779713,
12.5060906968582));
#165598=CARTESIAN_POINT('Ctrl Pts',(-20.7961362977383,-18.472547451059,
12.5163227455566));
#165599=CARTESIAN_POINT('Ctrl Pts',(-20.7904905713577,-18.448882400777,
12.5177311312538));
#165600=CARTESIAN_POINT('Ctrl Pts',(-20.7812755038438,-18.413006824194,
12.5198949244517));
#165601=CARTESIAN_POINT('Ctrl Pts',(-20.7780017676535,-18.4007220341299,
12.520641034919));
#165602=CARTESIAN_POINT('Ctrl Pts',(-20.7717115976596,-18.3779445800159,
12.5220344202404));
#165603=CARTESIAN_POINT('Ctrl Pts',(-20.7687242523026,-18.3674442791432,
12.5226807443555));
#165604=CARTESIAN_POINT('Ctrl Pts',(-20.7637102971677,-18.3503248196281,
12.5237411983776));
#165605=CARTESIAN_POINT('Ctrl Pts',(-20.7617321768065,-18.3436915827488,
12.5241537422371));
#165606=CARTESIAN_POINT('Ctrl Pts',(-20.7578487254815,-18.3308986332124,
12.5249526247701));
#165607=CARTESIAN_POINT('Ctrl Pts',(-20.7559477130758,-18.3247376819708,
12.525338818126));
#165608=CARTESIAN_POINT('Ctrl Pts',(-20.7515060164025,-18.3105726907948,
12.5262301456732));
#165609=CARTESIAN_POINT('Ctrl Pts',(-20.7489458046995,-18.3025749310625,
12.526735917306));
#165610=CARTESIAN_POINT('Ctrl Pts',(-20.7419616197391,-18.2811961882013,
12.5280947365095));
#165611=CARTESIAN_POINT('Ctrl Pts',(-20.7374515549886,-18.267843971008,
12.5289506103441));
#165612=CARTESIAN_POINT('Ctrl Pts',(-20.7294672453927,-18.2449622838481,
12.5304300016819));
#165613=CARTESIAN_POINT('Ctrl Pts',(-20.7260577868628,-18.2354125649028,
12.5310512601322));
#165614=CARTESIAN_POINT('Ctrl Pts',(-20.722580563326,-18.2258895792221,
12.5316746529861));
#165615=CARTESIAN_POINT('Origin',(-18.734,-18.952,0.));
#165616=CARTESIAN_POINT('',(-20.7225805759573,-18.2258896138153,13.5571445817067));
#165617=CARTESIAN_POINT('',(-20.7225805383928,-18.2258895109384,13.3344632701429));
#165618=CARTESIAN_POINT('',(-20.7225805737622,-18.2258896078036,0.));
#165619=CARTESIAN_POINT('Ctrl Pts',(-20.7225805759573,-18.2258896138153,
13.5571445817067));
#165620=CARTESIAN_POINT('Ctrl Pts',(-20.7282458896856,-18.2414050685604,
13.5562053219367));
#165621=CARTESIAN_POINT('Ctrl Pts',(-20.7337298095941,-18.2569873464273,
13.555260940775));
#165622=CARTESIAN_POINT('Ctrl Pts',(-20.7502231681677,-18.3056645889277,
13.5523055107353));
#165623=CARTESIAN_POINT('Ctrl Pts',(-20.7605967264764,-18.3389658822682,
13.5502759731478));
#165624=CARTESIAN_POINT('Ctrl Pts',(-20.7731190945415,-18.3829652423284,
13.5475782690586));
#165625=CARTESIAN_POINT('Ctrl Pts',(-20.7760149202605,-18.3934462461678,
13.5469344756048));
#165626=CARTESIAN_POINT('Ctrl Pts',(-20.7806193232447,-18.410625705192,
13.5458771253902));
#165627=CARTESIAN_POINT('Ctrl Pts',(-20.7823760851381,-18.4173111246253,
13.5454651366894));
#165628=CARTESIAN_POINT('Ctrl Pts',(-20.7857090369026,-18.4302523157076,
13.5446665855915));
#165629=CARTESIAN_POINT('Ctrl Pts',(-20.7872894372007,-18.4365069313526,
13.5442801645478));
#165630=CARTESIAN_POINT('Ctrl Pts',(-20.7908666319417,-18.4509415625605,
13.5433872364578));
#165631=CARTESIAN_POINT('Ctrl Pts',(-20.7928432511205,-18.4591264224568,
13.5428800845856));
#165632=CARTESIAN_POINT('Ctrl Pts',(-20.7980153369036,-18.4811173134203,
13.541515145064));
#165633=CARTESIAN_POINT('Ctrl Pts',(-20.8011210527526,-18.4949438180779,
13.5406544911353));
#165634=CARTESIAN_POINT('Ctrl Pts',(-20.8354181895579,-18.6551381146017,
13.5306529136224));
#165635=CARTESIAN_POINT('Ctrl Pts',(-20.8511375064961,-18.8043573065181,
13.5210013903412));
#165636=CARTESIAN_POINT('Ctrl Pts',(-20.8508605238589,-19.1037302303994,
13.5012718293646));
#165637=CARTESIAN_POINT('Ctrl Pts',(-20.8348287878723,-19.2530733054988,
13.4912566718935));
#165638=CARTESIAN_POINT('Ctrl Pts',(-20.799845502466,-19.4148371176257,
13.4809319276196));
#165639=CARTESIAN_POINT('Ctrl Pts',(-20.7963536193457,-19.4301562711893,
13.4799598356582));
#165640=CARTESIAN_POINT('Ctrl Pts',(-20.7913410447585,-19.4510695238938,
13.4786418671935));
#165641=CARTESIAN_POINT('Ctrl Pts',(-20.7899675522255,-19.4566979196881,
13.478288068359));
#165642=CARTESIAN_POINT('Ctrl Pts',(-20.787748533968,-19.4656317736744,
13.4777280102177));
#165643=CARTESIAN_POINT('Ctrl Pts',(-20.7869181050469,-19.4689408999646,
13.477520895203));
#165644=CARTESIAN_POINT('Ctrl Pts',(-20.7851867323183,-19.4757701709458,
13.4770941650689));
#165645=CARTESIAN_POINT('Ctrl Pts',(-20.7842847248748,-19.479290005506,
13.4768746186114));
#165646=CARTESIAN_POINT('Ctrl Pts',(-20.7821142206126,-19.4876700191264,
13.4763528244809));
#165647=CARTESIAN_POINT('Ctrl Pts',(-20.7808374701592,-19.4925280769787,
13.4760510525904));
#165648=CARTESIAN_POINT('Ctrl Pts',(-20.7764750802482,-19.508889938069,
13.4750369851723));
#165649=CARTESIAN_POINT('Ctrl Pts',(-20.773309589546,-19.5203724740291,
13.47432915802));
#165650=CARTESIAN_POINT('Ctrl Pts',(-20.7357651550015,-19.6522085472362,
13.4662400195074));
#165651=CARTESIAN_POINT('Ctrl Pts',(-20.6908691177103,-19.7693297597466,
13.4594084552319));
#165652=CARTESIAN_POINT('Ctrl Pts',(-20.5622083975088,-20.0324987574117,
13.4434863039871));
#165653=CARTESIAN_POINT('Ctrl Pts',(-20.4709010751107,-20.1738801990557,
13.4344328370744));
#165654=CARTESIAN_POINT('Ctrl Pts',(-20.348889543169,-20.321077046124,13.4233284249157));
#165655=CARTESIAN_POINT('Ctrl Pts',(-20.3336077474604,-20.3389012886101,
13.4219534251899));
#165656=CARTESIAN_POINT('Ctrl Pts',(-20.3116465903077,-20.3636702546708,
13.4199974279973));
#165657=CARTESIAN_POINT('Ctrl Pts',(-20.3052110899289,-20.3708295803461,
13.4194265848289));
#165658=CARTESIAN_POINT('Ctrl Pts',(-20.2946981018856,-20.3823657620718,
13.4184977063352));
#165659=CARTESIAN_POINT('Ctrl Pts',(-20.2906504534217,-20.3867697178529,
13.4181409371556));
#165660=CARTESIAN_POINT('Ctrl Pts',(-20.2821570943999,-20.395932485022,
13.4173940712192));
#165661=CARTESIAN_POINT('Ctrl Pts',(-20.2777079862541,-20.4006880485277,
13.4170038310379));
#165662=CARTESIAN_POINT('Ctrl Pts',(-20.2671051341271,-20.4119169221202,
13.4160761327725));
#165663=CARTESIAN_POINT('Ctrl Pts',(-20.2609322636243,-20.4183719276711,
13.415537850889));
#165664=CARTESIAN_POINT('Ctrl Pts',(-20.2401569124612,-20.4398234031783,
13.4137320977651));
#165665=CARTESIAN_POINT('Ctrl Pts',(-20.2253732572712,-20.4546419673749,
13.4124567171911));
#165666=CARTESIAN_POINT('Ctrl Pts',(-20.1447383594956,-20.5331050198639,
13.405548990035));
#165667=CARTESIAN_POINT('Ctrl Pts',(-20.0750375737915,-20.5926371448456,
13.3997423345331));
#165668=CARTESIAN_POINT('Ctrl Pts',(-19.926079420694,-20.7040141133195,
13.3876785909804));
#165669=CARTESIAN_POINT('Ctrl Pts',(-19.8467532240746,-20.7554370910499,
13.3814263045622));
#165670=CARTESIAN_POINT('Ctrl Pts',(-19.699414986957,-20.8375167701171,
13.370289089809));
#165671=CARTESIAN_POINT('Ctrl Pts',(-19.6327063455631,-20.8702095150086,
13.3654069591936));
#165672=CARTESIAN_POINT('Ctrl Pts',(-19.5255532159929,-20.9159036014132,
13.3579382545991));
#165673=CARTESIAN_POINT('Ctrl Pts',(-19.4862012041878,-20.9313099177001,
13.3552711407261));
#165674=CARTESIAN_POINT('Ctrl Pts',(-19.4393956539296,-20.9480364427922,
13.3522082547023));
#165675=CARTESIAN_POINT('Ctrl Pts',(-19.4323664128775,-20.9505066591476,
13.3517511352583));
#165676=CARTESIAN_POINT('Ctrl Pts',(-19.4209708582227,-20.9544438202842,
13.3510148638208));
#165677=CARTESIAN_POINT('Ctrl Pts',(-19.4166126125071,-20.9559336904233,
13.3507344058948));
#165678=CARTESIAN_POINT('Ctrl Pts',(-19.4088636489768,-20.9585544673733,
13.3502378005628));
#165679=CARTESIAN_POINT('Ctrl Pts',(-19.4054748994773,-20.9596910208718,
13.3500213229366));
#165680=CARTESIAN_POINT('Ctrl Pts',(-19.3981986907339,-20.9621109068194,
13.3495580108548));
#165681=CARTESIAN_POINT('Ctrl Pts',(-19.3943103938717,-20.9633915439031,
13.3493113358358));
#165682=CARTESIAN_POINT('Ctrl Pts',(-19.3836044856681,-20.9668832174273,
13.3486345926127));
#165683=CARTESIAN_POINT('Ctrl Pts',(-19.3767792499663,-20.9690709473955,
13.3482058752027));
#165684=CARTESIAN_POINT('Ctrl Pts',(-19.3399295312855,-20.9806765532009,
13.3459051925544));
#165685=CARTESIAN_POINT('Ctrl Pts',(-19.3097072904794,-20.9894593268456,
13.3440681888844));
#165686=CARTESIAN_POINT('Ctrl Pts',(-19.1212225761425,-21.039704830265,
13.332854818634));
#165687=CARTESIAN_POINT('Ctrl Pts',(-18.9587780067321,-21.0633834033794,
13.3242094820363));
#165688=CARTESIAN_POINT('Ctrl Pts',(-18.6781394689246,-21.0715014008406,
13.3088409863284));
#165689=CARTESIAN_POINT('Ctrl Pts',(-18.5610028730379,-21.0651666504295,
13.3023035224113));
#165690=CARTESIAN_POINT('Ctrl Pts',(-18.4308397089869,-21.047229617154,
13.2946061035415));
#165691=CARTESIAN_POINT('Ctrl Pts',(-18.416700190316,-21.0451349995879,
13.2937643733148));
#165692=CARTESIAN_POINT('Ctrl Pts',(-18.3942316634065,-21.0415736355259,
13.2924175042202));
#165693=CARTESIAN_POINT('Ctrl Pts',(-18.3858882071947,-21.0401998652864,
13.2919153085522));
#165694=CARTESIAN_POINT('Ctrl Pts',(-18.3711884698204,-21.037688971675,
13.2910268203547));
#165695=CARTESIAN_POINT('Ctrl Pts',(-18.3648287058661,-21.0365726773513,
13.2906411942171));
#165696=CARTESIAN_POINT('Ctrl Pts',(-18.3516858600685,-21.0342037549424,
13.2898416944674));
#165697=CARTESIAN_POINT('Ctrl Pts',(-18.3449036019305,-21.0329470367948,
13.289427694683));
#165698=CARTESIAN_POINT('Ctrl Pts',(-18.3275114010612,-21.029636351223,
13.2883623319934));
#165699=CARTESIAN_POINT('Ctrl Pts',(-18.3169109213849,-21.0275342644025,
13.2877094404035));
#165700=CARTESIAN_POINT('Ctrl Pts',(-18.2727439855553,-21.018423892853,
13.2849740035755));
#165701=CARTESIAN_POINT('Ctrl Pts',(-18.2393357423336,-21.010682071614,
13.2828681403017));
#165702=CARTESIAN_POINT('Ctrl Pts',(-18.1527992904461,-20.9884006606378,
13.2773138637222));
#165703=CARTESIAN_POINT('Ctrl Pts',(-18.1000270035709,-20.9725938076971,
13.2738270684348));
#165704=CARTESIAN_POINT('Ctrl Pts',(-17.9444687904138,-20.9193054686138,
13.2632580901603));
#165705=CARTESIAN_POINT('Ctrl Pts',(-17.8439125094339,-20.8758999792841,
13.2560275144735));
#165706=CARTESIAN_POINT('Ctrl Pts',(-17.7067697269938,-20.8036403685822,
13.2457875996755));
#165707=CARTESIAN_POINT('Ctrl Pts',(-17.6670698386887,-20.78105284497,13.2427768014387));
#165708=CARTESIAN_POINT('Ctrl Pts',(-17.6086456024531,-20.7452620088863,
13.2383013954012));
#165709=CARTESIAN_POINT('Ctrl Pts',(-17.5893545300633,-20.7330103742832,
13.2368161402139));
#165710=CARTESIAN_POINT('Ctrl Pts',(-17.5696671737039,-20.720055027991,
13.2352951669395));
#165711=CARTESIAN_POINT('Ctrl Pts',(-17.5690694103019,-20.7196612326977,
13.2352489809311));
#165712=CARTESIAN_POINT('Ctrl Pts',(-17.5587868246404,-20.7128797773917,
13.2344544155637));
#165713=CARTESIAN_POINT('Ctrl Pts',(-17.5491543110213,-20.7064128077944,
13.2337087918134));
#165714=CARTESIAN_POINT('Ctrl Pts',(-17.5066659675864,-20.677377915073,
13.2304157061503));
#165715=CARTESIAN_POINT('Ctrl Pts',(-17.4743958289856,-20.6539622734204,
13.2279032706524));
#165716=CARTESIAN_POINT('Ctrl Pts',(-17.437001712929,-20.6251820137652,
13.224996323079));
#165717=CARTESIAN_POINT('Ctrl Pts',(-17.4312226030626,-20.6206862094026,
13.2245471982384));
#165718=CARTESIAN_POINT('Ctrl Pts',(-17.4218767838708,-20.6133375703858,
13.2238212619225));
#165719=CARTESIAN_POINT('Ctrl Pts',(-17.4182958338883,-20.610503061577,
13.2235432022183));
#165720=CARTESIAN_POINT('Ctrl Pts',(-17.4119316343928,-20.605431881023,
13.2230492288381));
#165721=CARTESIAN_POINT('Ctrl Pts',(-17.4091448500313,-20.6031997398166,
13.2228329982393));
#165722=CARTESIAN_POINT('Ctrl Pts',(-17.4031550703202,-20.5983771566403,
13.2223684072554));
#165723=CARTESIAN_POINT('Ctrl Pts',(-17.3999539940804,-20.5957844212415,
13.2221202158317));
#165724=CARTESIAN_POINT('Ctrl Pts',(-17.3911140037175,-20.5885815746871,
13.2214350222382));
#165725=CARTESIAN_POINT('Ctrl Pts',(-17.3854912203313,-20.5839516304959,
13.2209994273968));
#165726=CARTESIAN_POINT('Ctrl Pts',(-17.3544049236562,-20.5580840084478,
13.2185917577018));
#165727=CARTESIAN_POINT('Ctrl Pts',(-17.3294176643107,-20.5362781180799,
13.2166586028926));
#165728=CARTESIAN_POINT('Ctrl Pts',(-17.1853104596759,-20.4044277265249,
13.2054514658538));
#165729=CARTESIAN_POINT('Ctrl Pts',(-17.0786307434889,-20.2815675355481,
13.1968792247434));
#165730=CARTESIAN_POINT('Ctrl Pts',(-16.921125726353,-20.0514479771962,
13.1816121712838));
#165731=CARTESIAN_POINT('Ctrl Pts',(-16.8633120122126,-19.9499079089429,
13.1750989154366));
#165732=CARTESIAN_POINT('Ctrl Pts',(-16.8081376511542,-19.831174243951,
13.1674287470711));
#165733=CARTESIAN_POINT('Ctrl Pts',(-16.802248074315,-19.8181568106517,
13.1665873678139));
#165734=CARTESIAN_POINT('Ctrl Pts',(-16.7930841113754,-19.7973437079106,
13.1652409554129));
#165735=CARTESIAN_POINT('Ctrl Pts',(-16.7897238189322,-19.7895861745453,
13.1647388623103));
#165736=CARTESIAN_POINT('Ctrl Pts',(-16.7838792514817,-19.77586877322,13.1638504935854));
#165737=CARTESIAN_POINT('Ctrl Pts',(-16.781375594216,-19.7699172438577,
13.1634648837798));
#165738=CARTESIAN_POINT('Ctrl Pts',(-16.7762533946041,-19.7575835261254,
13.1626653570131));
#165739=CARTESIAN_POINT('Ctrl Pts',(-16.7736387460745,-19.7511998128499,
13.1622513135794));
#165740=CARTESIAN_POINT('Ctrl Pts',(-16.7670070396622,-19.7347800157372,
13.1611857103279));
#165741=CARTESIAN_POINT('Ctrl Pts',(-16.7630356045105,-19.7247258271732,
13.1605326204928));
#165742=CARTESIAN_POINT('Ctrl Pts',(-16.746778326634,-19.6826276564685,
13.1577952623269));
#165743=CARTESIAN_POINT('Ctrl Pts',(-16.7351961508515,-19.6503192017796,
13.155687634972));
#165744=CARTESIAN_POINT('Ctrl Pts',(-16.7070664582551,-19.565407863023,
13.1501275958416));
#165745=CARTESIAN_POINT('Ctrl Pts',(-16.6917805320225,-19.5124173547892,
13.146636702717));
#165746=CARTESIAN_POINT('Ctrl Pts',(-16.6523815365308,-19.352657269505,
13.1360598530945));
#165747=CARTESIAN_POINT('Ctrl Pts',(-16.63445980609,-19.2445562920821,13.1288255301577));
#165748=CARTESIAN_POINT('Ctrl Pts',(-16.6206147033067,-19.0854858000645,
13.1182781000465));
#165749=CARTESIAN_POINT('Ctrl Pts',(-16.6180409145904,-19.0352663908553,
13.1149644091803));
#165750=CARTESIAN_POINT('Ctrl Pts',(-16.6170038677021,-18.9687499791338,
13.1106283038235));
#165751=CARTESIAN_POINT('Ctrl Pts',(-16.6169376580062,-18.9524954718793,
13.1095729175856));
#165752=CARTESIAN_POINT('Ctrl Pts',(-16.6174524777382,-18.8833362866789,
13.1051043759661));
#165753=CARTESIAN_POINT('Ctrl Pts',(-16.6198294737511,-18.8304593906509,
13.1017420235317));
#165754=CARTESIAN_POINT('Ctrl Pts',(-16.6249015871051,-18.7690559942071,
13.0979414686477));
#165755=CARTESIAN_POINT('Ctrl Pts',(-16.6256708945493,-18.7603935972077,
13.0974077384139));
#165756=CARTESIAN_POINT('Ctrl Pts',(-16.6269171871686,-18.7472780600256,
13.0966035606025));
#165757=CARTESIAN_POINT('Ctrl Pts',(-16.6273549489344,-18.7428214100118,
13.0963309899779));
#165758=CARTESIAN_POINT('Ctrl Pts',(-16.6281664661989,-18.7348207491394,
13.0958429437904));
#165759=CARTESIAN_POINT('Ctrl Pts',(-16.628535030248,-18.7312762794508,
13.0956271818577));
#165760=CARTESIAN_POINT('Ctrl Pts',(-16.6293557594768,-18.7235724965384,
13.0951592205105));
#165761=CARTESIAN_POINT('Ctrl Pts',(-16.6298113032941,-18.7194136013102,
13.0949072135247));
#165762=CARTESIAN_POINT('Ctrl Pts',(-16.6311266820552,-18.7077250677574,
13.0942006324703));
#165763=CARTESIAN_POINT('Ctrl Pts',(-16.6320146344134,-18.700198569024,
13.0937476134451));
#165764=CARTESIAN_POINT('Ctrl Pts',(-16.6375907064606,-18.6550207813029,
13.091039301309));
#165765=CARTESIAN_POINT('Ctrl Pts',(-16.6432502380772,-18.6174937694873,
13.0888352640505));
#165766=CARTESIAN_POINT('Ctrl Pts',(-16.6652823853798,-18.4940160236923,
13.0816749290102));
#165767=CARTESIAN_POINT('Ctrl Pts',(-16.6859735679076,-18.4089235330235,
13.0768864920537));
#165768=CARTESIAN_POINT('Ctrl Pts',(-16.7636144995826,-18.1583852342082,
13.0626164653763));
#165769=CARTESIAN_POINT('Ctrl Pts',(-16.8358276435823,-17.9984915360148,
13.053215739867));
#165770=CARTESIAN_POINT('Ctrl Pts',(-16.9388697291359,-17.8296242492804,
13.0417211504581));
#165771=CARTESIAN_POINT('Ctrl Pts',(-16.9511927996561,-17.8101513058842,
13.040371165572));
#165772=CARTESIAN_POINT('Ctrl Pts',(-16.9690714890971,-17.7828945104076,
13.0384448027332));
#165773=CARTESIAN_POINT('Ctrl Pts',(-16.9743660006824,-17.7749407498816,
13.0378781628341));
#165774=CARTESIAN_POINT('Ctrl Pts',(-16.9830548956979,-17.7620773706609,
13.0369542723203));
#165775=CARTESIAN_POINT('Ctrl Pts',(-16.9864165559753,-17.7571457297477,
13.0365982607901));
#165776=CARTESIAN_POINT('Ctrl Pts',(-16.9934959565628,-17.7468538561292,
13.0358514763955));
#165777=CARTESIAN_POINT('Ctrl Pts',(-16.9972177026315,-17.7414964670118,
13.0354605534526));
#165778=CARTESIAN_POINT('Ctrl Pts',(-17.0061287643284,-17.7287948417341,
13.034528464351));
#165779=CARTESIAN_POINT('Ctrl Pts',(-17.0113401998539,-17.721466345308,
13.0339864533244));
#165780=CARTESIAN_POINT('Ctrl Pts',(-17.0290463674991,-17.6969002584541,
13.0321551378376));
#165781=CARTESIAN_POINT('Ctrl Pts',(-17.0417540763313,-17.6798184358838,
13.0308576149445));
#165782=CARTESIAN_POINT('Ctrl Pts',(-17.1542173679943,-17.5333113050345,
13.0195137930639));
#165783=CARTESIAN_POINT('Ctrl Pts',(-17.2683722589163,-17.4156710659591,
13.0088618498842));
#165784=CARTESIAN_POINT('Ctrl Pts',(-17.4936222563106,-17.2317084714849,
12.9896460475969));
#165785=CARTESIAN_POINT('Ctrl Pts',(-17.5994478191215,-17.1601470007842,
12.9811957255661));
#165786=CARTESIAN_POINT('Ctrl Pts',(-17.7249440939048,-17.0908858119816,
12.9722520373462));
#165787=CARTESIAN_POINT('Ctrl Pts',(-17.7388963996446,-17.0833885633414,
12.9712719706824));
#165788=CARTESIAN_POINT('Ctrl Pts',(-17.7580828795255,-17.0733545938883,
12.9699449732795));
#165789=CARTESIAN_POINT('Ctrl Pts',(-17.763244904769,-17.0706820218648,
12.9695899827382));
#165790=CARTESIAN_POINT('Ctrl Pts',(-17.7714574672326,-17.0664728752481,
12.9690285051526));
#165791=CARTESIAN_POINT('Ctrl Pts',(-17.7745007832631,-17.0649223865919,
12.9688211548248));
#165792=CARTESIAN_POINT('Ctrl Pts',(-17.7807873482084,-17.0617386883837,
12.9683943275292));
#165793=CARTESIAN_POINT('Ctrl Pts',(-17.7840310478825,-17.0601064575698,
12.9681749175843));
#165794=CARTESIAN_POINT('Ctrl Pts',(-17.7917594566072,-17.0562424069358,
12.9676540732174));
#165795=CARTESIAN_POINT('Ctrl Pts',(-17.7962479525459,-17.0540181265502,
12.9673531098901));
#165796=CARTESIAN_POINT('Ctrl Pts',(-17.8113633772672,-17.0465943669352,
12.9663445888951));
#165797=CARTESIAN_POINT('Ctrl Pts',(-17.8220262065822,-17.041467933101,
12.9656414333361));
#165798=CARTESIAN_POINT('Ctrl Pts',(-17.9386649062282,-16.9865898466395,
12.9580336275535));
#165799=CARTESIAN_POINT('Ctrl Pts',(-18.0485655675198,-16.9456146416675,
12.9516101226785));
#165800=CARTESIAN_POINT('Ctrl Pts',(-18.3314767668379,-16.8661166397597,
12.935617175957));
#165801=CARTESIAN_POINT('Ctrl Pts',(-18.5069470991307,-16.8398033500741,
12.9261202882692));
#165802=CARTESIAN_POINT('Ctrl Pts',(-18.7065322400053,-16.8350543726336,
12.9145183136905));
#165803=CARTESIAN_POINT('Ctrl Pts',(-18.7294292767849,-16.8348811286629,
12.9131768029348));
#165804=CARTESIAN_POINT('Ctrl Pts',(-18.7618542938823,-16.8351617983587,
12.911260466604));
#165805=CARTESIAN_POINT('Ctrl Pts',(-18.7713838171537,-16.8353086480746,
12.9106952398952));
#165806=CARTESIAN_POINT('Ctrl Pts',(-18.7868744931945,-16.8356519998194,
12.9097730246598));
#165807=CARTESIAN_POINT('Ctrl Pts',(-18.7928364464923,-16.8358093560971,
12.9094172661618));
#165808=CARTESIAN_POINT('Ctrl Pts',(-18.8053216659356,-16.8361916856188,
12.908670499235));
#165809=CARTESIAN_POINT('Ctrl Pts',(-18.8118447067726,-16.8364216385625,
12.9082793384586));
#165810=CARTESIAN_POINT('Ctrl Pts',(-18.8273729830282,-16.8370409622449,
12.9073457331012));
#165811=CARTESIAN_POINT('Ctrl Pts',(-18.8363769452405,-16.8374576848649,
12.9068024363641));
#165812=CARTESIAN_POINT('Ctrl Pts',(-18.8667623768187,-16.8390585152533,
12.9049622477118));
#165813=CARTESIAN_POINT('Ctrl Pts',(-18.8881279175692,-16.8405095077609,
12.9036570286089));
#165814=CARTESIAN_POINT('Ctrl Pts',(-19.0047246468849,-16.8502069749094,
12.896470124863));
#165815=CARTESIAN_POINT('Ctrl Pts',(-19.0993233771937,-16.8645708848525,
12.8903979602762));
#165816=CARTESIAN_POINT('Ctrl Pts',(-19.3360518302462,-16.9171022305903,
12.874638198799));
#165817=CARTESIAN_POINT('Ctrl Pts',(-19.4757732903475,-16.9637734856989,
12.8647832448296));
#165818=CARTESIAN_POINT('Ctrl Pts',(-19.6204764948854,-17.0295034727646,
12.8544806231758));
#165819=CARTESIAN_POINT('Ctrl Pts',(-19.6313777229855,-17.0345676793184,
12.8537040930464));
#165820=CARTESIAN_POINT('Ctrl Pts',(-19.684638271346,-17.0598637811747,
12.8499101749084));
#165821=CARTESIAN_POINT('Ctrl Pts',(-19.7263632494966,-17.0814095823461,
12.8469377756625));
#165822=CARTESIAN_POINT('Ctrl Pts',(-19.774046542734,-17.1080772179113,
12.8435694545154));
#165823=CARTESIAN_POINT('Ctrl Pts',(-19.7807322571231,-17.1118642377903,
12.8430978536911));
#165824=CARTESIAN_POINT('Ctrl Pts',(-19.7914096780088,-17.1179893212938,
12.8423459502067));
#165825=CARTESIAN_POINT('Ctrl Pts',(-19.7954145253247,-17.1203041728711,
12.8420642165011));
#165826=CARTESIAN_POINT('Ctrl Pts',(-19.8024192482373,-17.1243836774142,
12.8415719957842));
#165827=CARTESIAN_POINT('Ctrl Pts',(-19.8054223979412,-17.1261426237375,
12.8413611439265));
#165828=CARTESIAN_POINT('Ctrl Pts',(-19.8117894489859,-17.1298929273187,
12.8409145053455));
#165829=CARTESIAN_POINT('Ctrl Pts',(-19.8151521698983,-17.1318861940101,
12.8406788454525));
#165830=CARTESIAN_POINT('Ctrl Pts',(-19.8220669391853,-17.1360108768627,
12.8401946904941));
#165831=CARTESIAN_POINT('Ctrl Pts',(-19.8256182943725,-17.1381434291685,
12.8399462698408));
#165832=CARTESIAN_POINT('Ctrl Pts',(-19.834471178125,-17.1434949120654,
12.8393275346212));
#165833=CARTESIAN_POINT('Ctrl Pts',(-19.8397649023677,-17.1467267658967,
12.8389580306695));
#165834=CARTESIAN_POINT('Ctrl Pts',(-19.8546646105452,-17.1559132648846,
12.8379191561724));
#165835=CARTESIAN_POINT('Ctrl Pts',(-19.8642373729619,-17.1619217274205,
12.8372530340652));
#165836=CARTESIAN_POINT('Ctrl Pts',(-19.8958505070486,-17.1821187998788,
12.8350560879775));
#165837=CARTESIAN_POINT('Ctrl Pts',(-19.9176762387845,-17.1966405643333,
12.833543963229));
#165838=CARTESIAN_POINT('Ctrl Pts',(-20.0759912279187,-17.3062715160992,
12.8225666700204));
#165839=CARTESIAN_POINT('Ctrl Pts',(-20.2011268501028,-17.4167761044752,
12.8137995936649));
#165840=CARTESIAN_POINT('Ctrl Pts',(-20.3826574391679,-17.6197688116501,
12.7988309613231));
#165841=CARTESIAN_POINT('Ctrl Pts',(-20.4472387654969,-17.7039134655659,
12.7928852697093));
#165842=CARTESIAN_POINT('Ctrl Pts',(-20.5129698561578,-17.8043266901874,
12.7858526703796));
#165843=CARTESIAN_POINT('Ctrl Pts',(-20.5205734975174,-17.8161994458466,
12.7850222646513));
#165844=CARTESIAN_POINT('Ctrl Pts',(-20.5325167209505,-17.8352649595421,
12.7836901381852));
#165845=CARTESIAN_POINT('Ctrl Pts',(-20.5369331453072,-17.8424092571693,
12.7831912595305));
#165846=CARTESIAN_POINT('Ctrl Pts',(-20.5446645848333,-17.8550841709679,
12.7823066273727));
#165847=CARTESIAN_POINT('Ctrl Pts',(-20.5479970846075,-17.8606040359401,
12.7819215216945));
#165848=CARTESIAN_POINT('Ctrl Pts',(-20.5548543643726,-17.8720804254847,
12.781121109729));
#165849=CARTESIAN_POINT('Ctrl Pts',(-20.5583752498665,-17.8780391768874,
12.7807056674335));
#165850=CARTESIAN_POINT('Ctrl Pts',(-20.5673726615341,-17.8934383358134,
12.7796323620631));
#165851=CARTESIAN_POINT('Ctrl Pts',(-20.5728054680181,-17.9029039334995,
12.7789729260842));
#165852=CARTESIAN_POINT('Ctrl Pts',(-20.595466542383,-17.9431032372606,
12.7761733581244));
#165853=CARTESIAN_POINT('Ctrl Pts',(-20.6119985375035,-17.9742210754947,
12.7740085190291));
#165854=CARTESIAN_POINT('Ctrl Pts',(-20.6533011646073,-18.0568794363104,
12.7682604816316));
#165855=CARTESIAN_POINT('Ctrl Pts',(-20.6767724033018,-18.1090336525876,
12.7646354791735));
#165856=CARTESIAN_POINT('Ctrl Pts',(-20.7066095078179,-18.1832214467718,
12.7594872233636));
#165857=CARTESIAN_POINT('Ctrl Pts',(-20.7147694497581,-18.2044974724095,
12.7580118269229));
#165858=CARTESIAN_POINT('Ctrl Pts',(-20.7225806094134,-18.2258897054408,
12.7565302021861));
#165859=CARTESIAN_POINT('Ctrl Pts',(-20.722580563326,-18.2258895792221,
12.5316746529861));
#165860=CARTESIAN_POINT('Ctrl Pts',(-20.6726392059308,-18.0891164249191,
12.5406280852242));
#165861=CARTESIAN_POINT('Ctrl Pts',(-20.6087205282652,-17.9578600560501,
12.5500631308234));
#165862=CARTESIAN_POINT('Ctrl Pts',(-20.495841044321,-17.7763075846016,
12.5641660621724));
#165863=CARTESIAN_POINT('Ctrl Pts',(-20.4570694493765,-17.7201849444968,
12.5686851501023));
#165864=CARTESIAN_POINT('Ctrl Pts',(-20.3695045829104,-17.605676700547,
12.578143339528));
#165865=CARTESIAN_POINT('Ctrl Pts',(-20.3201312863114,-17.5478449190529,
12.5830647942381));
#165866=CARTESIAN_POINT('Ctrl Pts',(-20.2570977371216,-17.4815915061845,
12.5887668295566));
#165867=CARTESIAN_POINT('Ctrl Pts',(-20.2463222522533,-17.4705111229829,
12.5897226874635));
#165868=CARTESIAN_POINT('Ctrl Pts',(-20.2323958720953,-17.4565009912937,
12.5909329936785));
#165869=CARTESIAN_POINT('Ctrl Pts',(-20.2293564012324,-17.4534618094339,
12.5911956468222));
#165870=CARTESIAN_POINT('Ctrl Pts',(-20.2234100628535,-17.4475521432674,
12.5917065391721));
#165871=CARTESIAN_POINT('Ctrl Pts',(-20.2205041026672,-17.4446807762249,
12.5919548464706));
#165872=CARTESIAN_POINT('Ctrl Pts',(-20.2150390814796,-17.4393119870393,
12.5924192353049));
#165873=CARTESIAN_POINT('Ctrl Pts',(-20.212482034711,-17.4368126654862,
12.5926354631504));
#165874=CARTESIAN_POINT('Ctrl Pts',(-20.2066071015656,-17.4310993913483,
12.593129859582));
#165875=CARTESIAN_POINT('Ctrl Pts',(-20.2032850258389,-17.4278898167287,
12.5934076862689));
#165876=CARTESIAN_POINT('Ctrl Pts',(-20.1929591289752,-17.417978741294,
12.5942659796904));
#165877=CARTESIAN_POINT('Ctrl Pts',(-20.1859196523087,-17.4113143430632,
12.5948436439327));
#165878=CARTESIAN_POINT('Ctrl Pts',(-20.1054372952489,-17.3361617773434,
12.6013673230243));
#165879=CARTESIAN_POINT('Ctrl Pts',(-20.0272461273801,-17.2729248900113,
12.6069500345036));
#165880=CARTESIAN_POINT('Ctrl Pts',(-19.8042374851132,-17.1174247970663,
12.6218252333107));
#165881=CARTESIAN_POINT('Ctrl Pts',(-19.6522468258273,-17.0368250357533,
12.630946333039));
#165882=CARTESIAN_POINT('Ctrl Pts',(-19.4517969301906,-16.9599333941322,
12.6432059230767));
#165883=CARTESIAN_POINT('Ctrl Pts',(-19.4109284029551,-16.9456776559222,
12.6457126382673));
#165884=CARTESIAN_POINT('Ctrl Pts',(-19.3584067042708,-16.9291445189173,
12.6489553371321));
#165885=CARTESIAN_POINT('Ctrl Pts',(-19.347130490564,-16.92569819061,12.6496527369484));
#165886=CARTESIAN_POINT('Ctrl Pts',(-19.3290044598153,-16.9203235195635,
12.6507759350379));
#165887=CARTESIAN_POINT('Ctrl Pts',(-19.3221725854135,-16.9183351711187,
12.6511997675783));
#165888=CARTESIAN_POINT('Ctrl Pts',(-19.3091831757126,-16.9146256625293,
12.652006577342));
#165889=CARTESIAN_POINT('Ctrl Pts',(-19.3030276024188,-16.9128978782556,
12.6523893334982));
#165890=CARTESIAN_POINT('Ctrl Pts',(-19.2890146527816,-16.9090330301002,
12.6532616502313));
#165891=CARTESIAN_POINT('Ctrl Pts',(-19.281152618338,-16.9069133724319,
12.653751770285));
#165892=CARTESIAN_POINT('Ctrl Pts',(-19.2607687325976,-16.9015436946763,
12.6550244059983));
#165893=CARTESIAN_POINT('Ctrl Pts',(-19.2482291098275,-16.8983630387472,
12.6558091509902));
#165894=CARTESIAN_POINT('Ctrl Pts',(-19.1667510125427,-16.8784892784045,
12.6609208404189));
#165895=CARTESIAN_POINT('Ctrl Pts',(-19.0970467100535,-16.8651565967857,
12.6653548976161));
#165896=CARTESIAN_POINT('Ctrl Pts',(-18.8701727638295,-16.8334722147435,
12.6799848545074));
#165897=CARTESIAN_POINT('Ctrl Pts',(-18.7115859575977,-16.8292210263562,
12.6905565333373));
#165898=CARTESIAN_POINT('Ctrl Pts',(-18.4973786524464,-16.8474971371102,
12.7046479156449));
#165899=CARTESIAN_POINT('Ctrl Pts',(-18.4409389667881,-16.8546116037792,
12.708336625622));
#165900=CARTESIAN_POINT('Ctrl Pts',(-18.3562334524621,-16.8687757483064,
12.7137752707624));
#165901=CARTESIAN_POINT('Ctrl Pts',(-18.3277158816484,-16.8741491253369,
12.7155892595651));
#165902=CARTESIAN_POINT('Ctrl Pts',(-18.2924798337307,-16.8815416604107,
12.7178019737823));
#165903=CARTESIAN_POINT('Ctrl Pts',(-18.2856504865096,-16.8830097849215,
12.7182294911942));
#165904=CARTESIAN_POINT('Ctrl Pts',(-18.2748697114186,-16.8853832457192,
12.7189021051901));
#165905=CARTESIAN_POINT('Ctrl Pts',(-18.2709134735501,-16.8862661592971,
12.7191484526767));
#165906=CARTESIAN_POINT('Ctrl Pts',(-18.2634665270089,-16.8879505631521,
12.7196112182471));
#165907=CARTESIAN_POINT('Ctrl Pts',(-18.2599753590175,-16.8887495384992,
12.7198277706465));
#165908=CARTESIAN_POINT('Ctrl Pts',(-18.2520106280811,-16.8905935991507,
12.720320931456));
#165909=CARTESIAN_POINT('Ctrl Pts',(-18.2475384343836,-16.8916443874431,
12.7205972089796));
#165910=CARTESIAN_POINT('Ctrl Pts',(-18.2357003146112,-16.8944665696313,
12.7213269389696));
#165911=CARTESIAN_POINT('Ctrl Pts',(-18.2283403396184,-16.8962629775936,
12.7217789915407));
#165912=CARTESIAN_POINT('Ctrl Pts',(-18.1775975456844,-16.9089371800601,
12.7248853376864));
#165913=CARTESIAN_POINT('Ctrl Pts',(-18.1345559281537,-16.9211487468151,
12.7274682464988));
#165914=CARTESIAN_POINT('Ctrl Pts',(-18.0851982777751,-16.9368585070135,
12.730403568002));
#165915=CARTESIAN_POINT('Ctrl Pts',(-18.0784769436947,-16.9390349143519,
12.7308027081704));
#165916=CARTESIAN_POINT('Ctrl Pts',(-18.0582336162471,-16.9457019662079,
12.7320034277663));
#165917=CARTESIAN_POINT('Ctrl Pts',(-18.044745778945,-16.9502955667868,
12.732801544856));
#165918=CARTESIAN_POINT('Ctrl Pts',(-17.8963569628164,-17.0025105735688,
12.741571219026));
#165919=CARTESIAN_POINT('Ctrl Pts',(-17.7665654491932,-17.0635537767595,
12.7491664376287));
#165920=CARTESIAN_POINT('Ctrl Pts',(-17.5642074657739,-17.18510422496,12.7621664916823));
#165921=CARTESIAN_POINT('Ctrl Pts',(-17.4877464683954,-17.2381783955783,
12.7673870748311));
#165922=CARTESIAN_POINT('Ctrl Pts',(-17.3985203725416,-17.3092497222161,
12.7740314606903));
#165923=CARTESIAN_POINT('Ctrl Pts',(-17.3822122522186,-17.322643026209,
12.7752699388119));
#165924=CARTESIAN_POINT('Ctrl Pts',(-17.3592685380076,-17.3420674851909,
12.7770483658151));
#165925=CARTESIAN_POINT('Ctrl Pts',(-17.3524664955446,-17.3479007302732,
12.7775802248401));
#165926=CARTESIAN_POINT('Ctrl Pts',(-17.3407813674926,-17.3580510295367,
12.7785020151554));
#165927=CARTESIAN_POINT('Ctrl Pts',(-17.335880771936,-17.3623478050028,
12.7788911022166));
#165928=CARTESIAN_POINT('Ctrl Pts',(-17.3265255808415,-17.3706270325755,
12.7796387159734));
#165929=CARTESIAN_POINT('Ctrl Pts',(-17.3220678450335,-17.3746058541631,
12.7799970884047));
#165930=CARTESIAN_POINT('Ctrl Pts',(-17.310498153287,-17.3850209008851,
12.7809328367908));
#165931=CARTESIAN_POINT('Ctrl Pts',(-17.3034130491469,-17.391486630634,
12.7815114574431));
#165932=CARTESIAN_POINT('Ctrl Pts',(-17.2792917200865,-17.4138016224707,
12.7835007981486));
#165933=CARTESIAN_POINT('Ctrl Pts',(-17.2624734614609,-17.4298830508599,
12.7849214292075));
#165934=CARTESIAN_POINT('Ctrl Pts',(-17.1239740107427,-17.5667557258532,
12.7969100999642));
#165935=CARTESIAN_POINT('Ctrl Pts',(-17.0171381398251,-17.7016205294686,
12.808145850001));
#165936=CARTESIAN_POINT('Ctrl Pts',(-16.8808749508392,-17.9245307106968,
12.8254101114445));
#165937=CARTESIAN_POINT('Ctrl Pts',(-16.8389294945554,-18.0041206017896,
12.8313402273036));
#165938=CARTESIAN_POINT('Ctrl Pts',(-16.786406127767,-18.1213061860514,
12.8395441228623));
#165939=CARTESIAN_POINT('Ctrl Pts',(-16.7716063354074,-18.1568989744915,
12.8419693529101));
#165940=CARTESIAN_POINT('Ctrl Pts',(-16.7550560170609,-18.1999842716596,
12.8448097528164));
#165941=CARTESIAN_POINT('Ctrl Pts',(-16.7523647584373,-18.2071048954922,
12.845276104228));
#165942=CARTESIAN_POINT('Ctrl Pts',(-16.7482513868724,-18.2181682686859,
12.845995745625));
#165943=CARTESIAN_POINT('Ctrl Pts',(-16.7468025082173,-18.2221009016467,
12.8462505900325));
#165944=CARTESIAN_POINT('Ctrl Pts',(-16.744143471165,-18.2293848259473,
12.8467207932211));
#165945=CARTESIAN_POINT('Ctrl Pts',(-16.7429301048028,-18.232734841755,
12.8469363373227));
#165946=CARTESIAN_POINT('Ctrl Pts',(-16.7402139764452,-18.2402934160427,
12.8474210746951));
#165947=CARTESIAN_POINT('Ctrl Pts',(-16.7387160833303,-18.2445036663757,
12.8476899767559));
#165948=CARTESIAN_POINT('Ctrl Pts',(-16.7343569286602,-18.2568802535473,
12.8484772970125));
#165949=CARTESIAN_POINT('Ctrl Pts',(-16.7315323510617,-18.2650595401201,
12.8489935902348));
#165950=CARTESIAN_POINT('Ctrl Pts',(-16.712149994112,-18.3223216616033,
12.8525815620223));
#165951=CARTESIAN_POINT('Ctrl Pts',(-16.6973469989159,-18.3719846977454,
12.8555577082946));
#165952=CARTESIAN_POINT('Ctrl Pts',(-16.6790029587518,-18.4429443200486,
12.8596848998645));
#165953=CARTESIAN_POINT('Ctrl Pts',(-16.6739428246946,-18.4638248237836,
12.8608842794552));
#165954=CARTESIAN_POINT('Ctrl Pts',(-16.6387823784657,-18.6192101247272,
12.8697214450266));
#165955=CARTESIAN_POINT('Ctrl Pts',(-16.621563652906,-18.7562927236294,
12.8770519057551));
#165956=CARTESIAN_POINT('Ctrl Pts',(-16.6153091136145,-18.9848146283761,
12.8896555702125));
#165957=CARTESIAN_POINT('Ctrl Pts',(-16.618663875674,-19.0756050852872,
12.8947579560401));
#165958=CARTESIAN_POINT('Ctrl Pts',(-16.6299380784356,-19.1866197428317,
12.9012593381151));
#165959=CARTESIAN_POINT('Ctrl Pts',(-16.6323486772578,-19.2073128775864,
12.9024822090889));
#165960=CARTESIAN_POINT('Ctrl Pts',(-16.6362262795873,-19.2368049976816,
12.9042420904617));
#165961=CARTESIAN_POINT('Ctrl Pts',(-16.6374441552643,-19.2456359224618,
12.9047712433211));
#165962=CARTESIAN_POINT('Ctrl Pts',(-16.6396477488413,-19.2609013094936,
12.9056898380959));
#165963=CARTESIAN_POINT('Ctrl Pts',(-16.6406074421037,-19.2673394488882,
12.9060784517288));
#165964=CARTESIAN_POINT('Ctrl Pts',(-16.6425065337519,-19.2796887304405,
12.9068262102084));
#165965=CARTESIAN_POINT('Ctrl Pts',(-16.6434413394955,-19.2856005234742,
12.9071852058547));
#165966=CARTESIAN_POINT('Ctrl Pts',(-16.6459483195019,-19.3010304365752,
12.9081249274343));
#165967=CARTESIAN_POINT('Ctrl Pts',(-16.6475604935405,-19.3105418345919,
12.9087069188967));
#165968=CARTESIAN_POINT('Ctrl Pts',(-16.6533404996115,-19.3432825195913,
12.9107198583121));
#165969=CARTESIAN_POINT('Ctrl Pts',(-16.6578316029644,-19.3664522688008,
12.9121610358039));
#165970=CARTESIAN_POINT('Ctrl Pts',(-16.6968555617556,-19.5511890244566,
12.9237897721436));
#165971=CARTESIAN_POINT('Ctrl Pts',(-16.7498014422358,-19.7082547965098,
12.9345918435711));
#165972=CARTESIAN_POINT('Ctrl Pts',(-16.8749489375303,-19.9727123861095,
12.9539263690238));
#165973=CARTESIAN_POINT('Ctrl Pts',(-16.9397446874142,-20.0827427822681,
12.9623537958568));
#165974=CARTESIAN_POINT('Ctrl Pts',(-17.0210404623721,-20.1960266799001,
12.9710016065529));
#165975=CARTESIAN_POINT('Ctrl Pts',(-17.0281138164715,-20.2057085394788,
12.9717403102875));
#165976=CARTESIAN_POINT('Ctrl Pts',(-17.0382747871505,-20.2193714407553,
12.9727815941784));
#165977=CARTESIAN_POINT('Ctrl Pts',(-17.0412947915898,-20.2234021570532,
12.9730886394964));
#165978=CARTESIAN_POINT('Ctrl Pts',(-17.0465196850856,-20.2303240615779,
12.9736156177129));
#165979=CARTESIAN_POINT('Ctrl Pts',(-17.0487176812485,-20.2332204051271,
12.9738360281671));
#165980=CARTESIAN_POINT('Ctrl Pts',(-17.0529903612111,-20.2388205814184,
12.9742619969251));
#165981=CARTESIAN_POINT('Ctrl Pts',(-17.0550641121286,-20.2415250673253,
12.974467620431));
#165982=CARTESIAN_POINT('Ctrl Pts',(-17.0606692276946,-20.2487985472894,
12.9750204221127));
#165983=CARTESIAN_POINT('Ctrl Pts',(-17.0642128007345,-20.2533581585189,
12.9753667446415));
#165984=CARTESIAN_POINT('Ctrl Pts',(-17.0773899300473,-20.2701710896825,
12.9766431860674));
#165985=CARTESIAN_POINT('Ctrl Pts',(-17.0871403354192,-20.2823327488407,
12.9775653668179));
#165986=CARTESIAN_POINT('Ctrl Pts',(-17.1836989037092,-20.4000813033934,
12.9864949800968));
#165987=CARTESIAN_POINT('Ctrl Pts',(-17.2804189429874,-20.4971490008717,
12.9938783338125));
#165988=CARTESIAN_POINT('Ctrl Pts',(-17.5049775028981,-20.6826273943054,
13.009694925083));
#165989=CARTESIAN_POINT('Ctrl Pts',(-17.6345178232724,-20.7676814038846,
13.0181143961081));
#165990=CARTESIAN_POINT('Ctrl Pts',(-17.7911005499161,-20.8475426771301,
13.0283508932813));
#165991=CARTESIAN_POINT('Ctrl Pts',(-17.8101924719464,-20.8569202125973,
13.0295990641214));
#165992=CARTESIAN_POINT('Ctrl Pts',(-17.8375492462544,-20.8698492778496,
13.0313889988085));
#165993=CARTESIAN_POINT('Ctrl Pts',(-17.8457008244117,-20.87363846165,13.031922526823));
#165994=CARTESIAN_POINT('Ctrl Pts',(-17.8598084670379,-20.8800873188591,
13.032846291248));
#165995=CARTESIAN_POINT('Ctrl Pts',(-17.8657531893988,-20.8827716125581,
13.0332356735642));
#165996=CARTESIAN_POINT('Ctrl Pts',(-17.8771616926128,-20.8878596915624,
13.0339832119924));
#165997=CARTESIAN_POINT('Ctrl Pts',(-17.8826234286354,-20.8902679285949,
13.0343412107489));
#165998=CARTESIAN_POINT('Ctrl Pts',(-17.8968576482662,-20.8964724350867,
13.0352745664545));
#165999=CARTESIAN_POINT('Ctrl Pts',(-17.9056457156943,-20.9002324150017,
13.0358511555999));
#166000=CARTESIAN_POINT('Ctrl Pts',(-17.9357273945377,-20.9128625503068,
13.0378261756929));
#166001=CARTESIAN_POINT('Ctrl Pts',(-17.9571397905482,-20.9214438917476,
13.0392343262504));
#166002=CARTESIAN_POINT('Ctrl Pts',(-18.1416936390911,-20.9919286503674,
13.051395127585));
#166003=CARTESIAN_POINT('Ctrl Pts',(-18.311742252086,-21.0337807434095,
13.0628424359433));
#166004=CARTESIAN_POINT('Ctrl Pts',(-18.5720581558695,-21.0646185849479,
13.0801628309152));
#166005=CARTESIAN_POINT('Ctrl Pts',(-18.65972413674,-21.0695144574044,13.085945321539));
#166006=CARTESIAN_POINT('Ctrl Pts',(-18.7854445783979,-21.0687159538271,
13.0939733905083));
#166007=CARTESIAN_POINT('Ctrl Pts',(-18.8234329046947,-21.0674515226767,
13.0963639509826));
#166008=CARTESIAN_POINT('Ctrl Pts',(-18.8689372444367,-21.0647087882098,
13.0991692345239));
#166009=CARTESIAN_POINT('Ctrl Pts',(-18.8765029382357,-21.0642119686014,
13.0996337111039));
#166010=CARTESIAN_POINT('Ctrl Pts',(-18.8882398367112,-21.0633778871278,
13.1003510876822));
#166011=CARTESIAN_POINT('Ctrl Pts',(-18.8924128967652,-21.0630688914194,
13.1006055268134));
#166012=CARTESIAN_POINT('Ctrl Pts',(-18.9001380748592,-21.0624738422768,
13.1010753540193));
#166013=CARTESIAN_POINT('Ctrl Pts',(-18.9036903563048,-21.0621911956339,
13.1012909250337));
#166014=CARTESIAN_POINT('Ctrl Pts',(-18.9117040925988,-21.061533194822,
13.1017761907375));
#166015=CARTESIAN_POINT('Ctrl Pts',(-18.9161650676059,-21.0611526577214,
13.1020455913726));
#166016=CARTESIAN_POINT('Ctrl Pts',(-18.9292829714867,-21.0599917246666,
13.1028357275256));
#166017=CARTESIAN_POINT('Ctrl Pts',(-18.9379364610194,-21.0591721514735,
13.1033543152021));
#166018=CARTESIAN_POINT('Ctrl Pts',(-18.9990565437284,-21.0530034165173,
13.1069999924302));
#166019=CARTESIAN_POINT('Ctrl Pts',(-19.0513168291057,-21.0457481572747,
13.1100280163762));
#166020=CARTESIAN_POINT('Ctrl Pts',(-19.1188001538871,-21.033794189404,
13.1138841966698));
#166021=CARTESIAN_POINT('Ctrl Pts',(-19.1343133969745,-21.0308668565553,
13.1147669153121));
#166022=CARTESIAN_POINT('Ctrl Pts',(-19.1996437267442,-21.0177806647656,
13.1184736760663));
#166023=CARTESIAN_POINT('Ctrl Pts',(-19.2491205902866,-21.0060021812644,
13.1212551280918));
#166024=CARTESIAN_POINT('Ctrl Pts',(-19.4035796404331,-20.9632986832349,
13.1299803013965));
#166025=CARTESIAN_POINT('Ctrl Pts',(-19.5066126262187,-20.9260132069043,
13.1358712809829));
#166026=CARTESIAN_POINT('Ctrl Pts',(-19.6565774838452,-20.8581964114394,
13.1450223352114));
#166027=CARTESIAN_POINT('Ctrl Pts',(-19.7059453743396,-20.8335035249732,
13.1481337027462));
#166028=CARTESIAN_POINT('Ctrl Pts',(-19.784378474871,-20.7903615760218,
13.15328351995));
#166029=CARTESIAN_POINT('Ctrl Pts',(-19.8140584783427,-20.7730825656447,
13.1552824652543));
#166030=CARTESIAN_POINT('Ctrl Pts',(-19.8525132550122,-20.749424271264,
13.157945208757));
#166031=CARTESIAN_POINT('Ctrl Pts',(-19.8616788915706,-20.7436880932539,
13.158585431278));
#166032=CARTESIAN_POINT('Ctrl Pts',(-19.8766199786655,-20.7341773706232,
13.1596384030966));
#166033=CARTESIAN_POINT('Ctrl Pts',(-19.8824217027545,-20.7304443165073,
13.1600496095859));
#166034=CARTESIAN_POINT('Ctrl Pts',(-19.8936175178687,-20.7231628662304,
13.160847705117));
#166035=CARTESIAN_POINT('Ctrl Pts',(-19.8990138328306,-20.7196180170903,
13.1612344584391));
#166036=CARTESIAN_POINT('Ctrl Pts',(-19.9114372707823,-20.7113754352052,
13.1621296962606));
#166037=CARTESIAN_POINT('Ctrl Pts',(-19.9184526074928,-20.7066602138298,
13.1626388362401));
#166038=CARTESIAN_POINT('Ctrl Pts',(-19.937245773135,-20.6938646950458,
13.1640126083004));
#166039=CARTESIAN_POINT('Ctrl Pts',(-19.9489702189492,-20.685707114188,
13.1648801648937));
#166040=CARTESIAN_POINT('Ctrl Pts',(-20.0755780798838,-20.5957014666802,
13.1743651431348));
#166041=CARTESIAN_POINT('Ctrl Pts',(-20.1820673884184,-20.5027010496833,
13.1834322607992));
#166042=CARTESIAN_POINT('Ctrl Pts',(-20.3445945972032,-20.3293207961588,
13.1990666404115));
#166043=CARTESIAN_POINT('Ctrl Pts',(-20.4057792723084,-20.2543754434638,
13.2054948121062));
#166044=CARTESIAN_POINT('Ctrl Pts',(-20.4993339321267,-20.1222738997033,
13.2160579507907));
#166045=CARTESIAN_POINT('Ctrl Pts',(-20.5345603034473,-20.0673157048691,
13.2202520750685));
#166046=CARTESIAN_POINT('Ctrl Pts',(-20.5737749635816,-19.9994207242408,
13.2251235166052));
#166047=CARTESIAN_POINT('Ctrl Pts',(-20.5802489458008,-19.9879666695039,
13.2259351052215));
#166048=CARTESIAN_POINT('Ctrl Pts',(-20.5891459492004,-19.9718773660392,
13.2270601035786));
#166049=CARTESIAN_POINT('Ctrl Pts',(-20.5916590623751,-19.9672926395438,
13.2273789882407));
#166050=CARTESIAN_POINT('Ctrl Pts',(-20.5959079053943,-19.959472793484,
13.2279199561409));
#166051=CARTESIAN_POINT('Ctrl Pts',(-20.597652242804,-19.9562423992223,
13.2281425834928));
#166052=CARTESIAN_POINT('Ctrl Pts',(-20.6009776731424,-19.9500454237942,
13.2285680129199));
#166053=CARTESIAN_POINT('Ctrl Pts',(-20.6025601087368,-19.9470796050424,
13.2287709030964));
#166054=CARTESIAN_POINT('Ctrl Pts',(-20.6067291654819,-19.9392208989337,
13.2293066524614));
#166055=CARTESIAN_POINT('Ctrl Pts',(-20.6093036956872,-19.9343215772095,
13.2296387490427));
#166056=CARTESIAN_POINT('Ctrl Pts',(-20.6183487932644,-19.9169436287297,
13.2308101746344));
#166057=CARTESIAN_POINT('Ctrl Pts',(-20.624714422573,-19.9044104037931,
13.2316431587626));
#166058=CARTESIAN_POINT('Ctrl Pts',(-20.7038354065135,-19.7447097740224,
13.2421192210842));
#166059=CARTESIAN_POINT('Ctrl Pts',(-20.7593686541722,-19.5896039360084,
13.2508474239028));
#166060=CARTESIAN_POINT('Ctrl Pts',(-20.8270296741189,-19.2974350214183,
13.2671777061719));
#166061=CARTESIAN_POINT('Ctrl Pts',(-20.8448588559151,-19.1626336171357,
13.2746744187749));
#166062=CARTESIAN_POINT('Ctrl Pts',(-20.8502665616344,-19.0102153568468,
13.2835989852316));
#166063=CARTESIAN_POINT('Ctrl Pts',(-20.8506630232661,-18.9933619287538,
13.2845914868813));
#166064=CARTESIAN_POINT('Ctrl Pts',(-20.8509528941037,-18.9683224475064,
13.2860751767025));
#166065=CARTESIAN_POINT('Ctrl Pts',(-20.8510001744628,-18.9601385869792,
13.2865615472164));
#166066=CARTESIAN_POINT('Ctrl Pts',(-20.8509998627402,-18.9455564775112,
13.287430820218));
#166067=CARTESIAN_POINT('Ctrl Pts',(-20.8509707194824,-18.9391582988112,
13.2878131398688));
#166068=CARTESIAN_POINT('Ctrl Pts',(-20.8508481156793,-18.9256683307239,
13.2886211834744));
#166069=CARTESIAN_POINT('Ctrl Pts',(-20.8507480205214,-18.918576694131,
13.2890471107737));
#166070=CARTESIAN_POINT('Ctrl Pts',(-20.8503886243578,-18.8998005217454,
13.2901779006967));
#166071=CARTESIAN_POINT('Ctrl Pts',(-20.8500681972661,-18.8881175237119,
13.2908846698275));
#166072=CARTESIAN_POINT('Ctrl Pts',(-20.8481220039088,-18.8336263276935,
13.2941963139784));
#166073=CARTESIAN_POINT('Ctrl Pts',(-20.8452939285612,-18.7908736457192,
13.2968385575518));
#166074=CARTESIAN_POINT('Ctrl Pts',(-20.8339020495849,-18.6730661298717,
13.3042463415294));
#166075=CARTESIAN_POINT('Ctrl Pts',(-20.8226163019958,-18.5983437869904,
13.3090901552408));
#166076=CARTESIAN_POINT('Ctrl Pts',(-20.7864357517189,-18.422914129632,
13.32076528655));
#166077=CARTESIAN_POINT('Ctrl Pts',(-20.7580935482861,-18.3231480981609,
13.3276519677475));
#166078=CARTESIAN_POINT('Ctrl Pts',(-20.7225805383928,-18.2258895109384,
13.3344632701429));
#166079=CARTESIAN_POINT('Origin',(-18.734,-18.952,0.));
#166080=CARTESIAN_POINT('',(-20.7249097977618,-18.2250590878524,14.355439975907));
#166081=CARTESIAN_POINT('',(-20.7225805482453,-18.2258895379212,14.1348940720942));
#166082=CARTESIAN_POINT('',(-20.7225805737622,-18.2258896078036,0.));
#166083=CARTESIAN_POINT('',(-20.8478582366632,-18.9515402791097,14.3110888556867));
#166084=CARTESIAN_POINT('Ctrl Pts',(-20.8476070208165,-18.9515314190756,
14.3109441065097));
#166085=CARTESIAN_POINT('Ctrl Pts',(-20.8480883129925,-18.7039932788114,
14.3257760629755));
#166086=CARTESIAN_POINT('Ctrl Pts',(-20.8073980168978,-18.4566058676403,
14.3406080194413));
#166087=CARTESIAN_POINT('Ctrl Pts',(-20.7249097977618,-18.2250590878524,
14.355439975907));
#166088=CARTESIAN_POINT('Ctrl Pts',(-20.8509999712464,-18.9516510837263,
14.3128991057222));
#166089=CARTESIAN_POINT('Ctrl Pts',(-20.8510014360955,-18.9605388474593,
14.312378540246));
#166090=CARTESIAN_POINT('Ctrl Pts',(-20.8509469309215,-18.9694264524988,
14.3118562864048));
#166091=CARTESIAN_POINT('Ctrl Pts',(-20.8507292584146,-18.9869375893009,
14.3108238157218));
#166092=CARTESIAN_POINT('Ctrl Pts',(-20.8505693532511,-18.9955609702645,
14.3103137106949));
#166093=CARTESIAN_POINT('Ctrl Pts',(-20.8502036146175,-19.0103940167029,
14.3094333214644));
#166094=CARTESIAN_POINT('Ctrl Pts',(-20.850023130942,-19.016604239536,14.3090638320091));
#166095=CARTESIAN_POINT('Ctrl Pts',(-20.8496088606317,-19.0289820929612,
14.3083255693495));
#166096=CARTESIAN_POINT('Ctrl Pts',(-20.8493754333867,-19.0351496746715,
14.3079568109861));
#166097=CARTESIAN_POINT('Ctrl Pts',(-20.8488557235166,-19.0474570436085,
14.3072191250324));
#166098=CARTESIAN_POINT('Ctrl Pts',(-20.8485696657882,-19.0535967802356,
14.3068502080422));
#166099=CARTESIAN_POINT('Ctrl Pts',(-20.8477228783011,-19.0702146299458,
14.3058491893612));
#166100=CARTESIAN_POINT('Ctrl Pts',(-20.8471109811983,-19.0806898594257,
14.3052154881987));
#166101=CARTESIAN_POINT('Ctrl Pts',(-20.8445147262455,-19.1201005063434,
14.3028209232233));
#166102=CARTESIAN_POINT('Ctrl Pts',(-20.8420137567466,-19.1489976149218,
14.3010439561728));
#166103=CARTESIAN_POINT('Ctrl Pts',(-20.815907258728,-19.3923281087132,
14.2858946196423));
#166104=CARTESIAN_POINT('Ctrl Pts',(-20.7602432250021,-19.6020196557498,
14.2714263286646));
#166105=CARTESIAN_POINT('Ctrl Pts',(-20.6467520636624,-19.8617627039859,
14.2529056809952));
#166106=CARTESIAN_POINT('Ctrl Pts',(-20.6166241201534,-19.9225755266126,
14.2485387040674));
#166107=CARTESIAN_POINT('Ctrl Pts',(-20.5770943855693,-19.9935720493767,
14.2434879589216));
#166108=CARTESIAN_POINT('Ctrl Pts',(-20.5704516718481,-20.0052400136454,
14.2426595268361));
#166109=CARTESIAN_POINT('Ctrl Pts',(-20.5610470376768,-20.0213997863401,
14.2415153069965));
#166110=CARTESIAN_POINT('Ctrl Pts',(-20.558378825691,-20.0259453815967,
14.2411937972707));
#166111=CARTESIAN_POINT('Ctrl Pts',(-20.5538191683491,-20.0336472313171,
14.2406497024673));
#166112=CARTESIAN_POINT('Ctrl Pts',(-20.5519364303086,-20.0368085889079,
14.2404265583759));
#166113=CARTESIAN_POINT('Ctrl Pts',(-20.5483224687521,-20.04284106053,14.2400011420792));
#166114=CARTESIAN_POINT('Ctrl Pts',(-20.5465926605702,-20.0457129820781,
14.2397987769742));
#166115=CARTESIAN_POINT('Ctrl Pts',(-20.5420136668464,-20.053274575647,
14.2392663669325));
#166116=CARTESIAN_POINT('Ctrl Pts',(-20.5391530354266,-20.0579573367416,
14.2389370667533));
#166117=CARTESIAN_POINT('Ctrl Pts',(-20.5290469898277,-20.0743569314511,
14.2377850743866));
#166118=CARTESIAN_POINT('Ctrl Pts',(-20.5217052701548,-20.0860144031987,
14.2369684545243));
#166119=CARTESIAN_POINT('Ctrl Pts',(-20.4236098853709,-20.2384536124661,
14.2263084073253));
#166120=CARTESIAN_POINT('Ctrl Pts',(-20.3165592300704,-20.3680749711931,
14.2174199495125));
#166121=CARTESIAN_POINT('Ctrl Pts',(-20.1071165397495,-20.5678912026601,
14.201648127221));
#166122=CARTESIAN_POINT('Ctrl Pts',(-20.0118088457996,-20.6442626566637,
14.1949126375874));
#166123=CARTESIAN_POINT('Ctrl Pts',(-19.8967870552831,-20.7211483787345,
14.1868799981298));
#166124=CARTESIAN_POINT('Ctrl Pts',(-19.8830022008332,-20.7301320654897,
14.1859191076192));
#166125=CARTESIAN_POINT('Ctrl Pts',(-19.860972871489,-20.7441256026124,
14.184385580337));
#166126=CARTESIAN_POINT('Ctrl Pts',(-19.8527962948688,-20.7492414625177,
14.1838168278146));
#166127=CARTESIAN_POINT('Ctrl Pts',(-19.8372243392276,-20.75883696328,14.1827343413239));
#166128=CARTESIAN_POINT('Ctrl Pts',(-19.8298359015976,-20.7633275319303,
14.1822210199465));
#166129=CARTESIAN_POINT('Ctrl Pts',(-19.8169494055923,-20.7710520248803,
14.1813261175671));
#166130=CARTESIAN_POINT('Ctrl Pts',(-19.8114638196377,-20.7743066153345,
14.1809452973286));
#166131=CARTESIAN_POINT('Ctrl Pts',(-19.800801872806,-20.7805673614268,
14.1802053303951));
#166132=CARTESIAN_POINT('Ctrl Pts',(-19.7956273000035,-20.7835764537254,
14.1798462951409));
#166133=CARTESIAN_POINT('Ctrl Pts',(-19.7820770209202,-20.7913794311546,
14.1789063217241));
#166134=CARTESIAN_POINT('Ctrl Pts',(-19.773681243935,-20.7961380207893,
14.178324116709));
#166135=CARTESIAN_POINT('Ctrl Pts',(-19.7446895773684,-20.812309116856,
14.1763142087727));
#166136=CARTESIAN_POINT('Ctrl Pts',(-19.7239365761549,-20.8234349940621,
14.1748763337507));
#166137=CARTESIAN_POINT('Ctrl Pts',(-19.555430641894,-20.9101854463847,
14.1632041284054));
#166138=CARTESIAN_POINT('Ctrl Pts',(-19.3994619530342,-20.9685264577361,
14.152348894216));
#166139=CARTESIAN_POINT('Ctrl Pts',(-19.1152559846428,-21.0382378526541,
14.1330105284854));
#166140=CARTESIAN_POINT('Ctrl Pts',(-18.9897188576312,-21.057316856051,
14.1246326210804));
#166141=CARTESIAN_POINT('Ctrl Pts',(-18.8512577411353,-21.0657840985883,
14.1160292893991));
#166142=CARTESIAN_POINT('Ctrl Pts',(-18.8392907274131,-21.066413978212,
14.1152910141762));
#166143=CARTESIAN_POINT('Ctrl Pts',(-18.8222882584098,-21.0671641870112,
14.1142502251586));
#166144=CARTESIAN_POINT('Ctrl Pts',(-18.8172569832257,-21.0673682021185,
14.1139432518533));
#166145=CARTESIAN_POINT('Ctrl Pts',(-18.8085917741356,-21.067688607849,
14.1134163580798));
#166146=CARTESIAN_POINT('Ctrl Pts',(-18.8049581960322,-21.0678135913507,
14.1131959604581));
#166147=CARTESIAN_POINT('Ctrl Pts',(-18.7979176584284,-21.0680376058945,
14.1127699857626));
#166148=CARTESIAN_POINT('Ctrl Pts',(-18.7945107816376,-21.0681377701615,
14.112564343633));
#166149=CARTESIAN_POINT('Ctrl Pts',(-18.785329555893,-21.0683855133529,
14.1120114270799));
#166150=CARTESIAN_POINT('Ctrl Pts',(-18.7795547712931,-21.068517689279,
14.1116650089419));
#166151=CARTESIAN_POINT('Ctrl Pts',(-18.7581848562079,-21.0689193111002,
14.1103878415527));
#166152=CARTESIAN_POINT('Ctrl Pts',(-18.7425869945597,-21.0690400498063,
14.1094650421133));
#166153=CARTESIAN_POINT('Ctrl Pts',(-18.5906053038285,-21.0685366994878,
14.1005528397399));
#166154=CARTESIAN_POINT('Ctrl Pts',(-18.4545648530217,-21.05490654891,14.0931846465046));
#166155=CARTESIAN_POINT('Ctrl Pts',(-18.1689284329872,-20.9980575117669,
14.0773689311472));
#166156=CARTESIAN_POINT('Ctrl Pts',(-18.0208832086587,-20.9512784175718,
14.0689349670101));
#166157=CARTESIAN_POINT('Ctrl Pts',(-17.8598079324731,-20.8801933712459,
14.0586815360964));
#166158=CARTESIAN_POINT('Ctrl Pts',(-17.8404789674107,-20.8713127842066,
14.057433318977));
#166159=CARTESIAN_POINT('Ctrl Pts',(-17.8131765986745,-20.8582670517137,
14.0556433293685));
#166160=CARTESIAN_POINT('Ctrl Pts',(-17.8050904620997,-20.8543398422678,
14.0551097934122));
#166161=CARTESIAN_POINT('Ctrl Pts',(-17.791180615331,-20.8474743874975,
14.054186019593));
#166162=CARTESIAN_POINT('Ctrl Pts',(-17.7853449785908,-20.8445604863923,
14.0537966358714));
#166163=CARTESIAN_POINT('Ctrl Pts',(-17.7741949792,-20.8389284438281,14.0530490977907));
#166164=CARTESIAN_POINT('Ctrl Pts',(-17.7688784561684,-20.8362146997035,
14.052691100802));
#166165=CARTESIAN_POINT('Ctrl Pts',(-17.7550784322163,-20.8290969418229,
14.0517577564098));
#166166=CARTESIAN_POINT('Ctrl Pts',(-17.7466132250411,-20.824657928406,
14.0511811768692));
#166167=CARTESIAN_POINT('Ctrl Pts',(-17.71782353978,-20.8093116193805,14.0492062246067));
#166168=CARTESIAN_POINT('Ctrl Pts',(-17.6976479570919,-20.7981298510406,
14.047798133178));
#166169=CARTESIAN_POINT('Ctrl Pts',(-17.5264449751161,-20.6995543916272,
14.035637443227));
#166170=CARTESIAN_POINT('Ctrl Pts',(-17.3866017638648,-20.5941420245203,
14.024190190605));
#166171=CARTESIAN_POINT('Ctrl Pts',(-17.1982886047833,-20.4117853370239,
14.006869735388));
#166172=CARTESIAN_POINT('Ctrl Pts',(-17.1391261069682,-20.3469057028291,
14.0010871382322));
#166173=CARTESIAN_POINT('Ctrl Pts',(-17.0603452764371,-20.248924388656,
13.9930589421129));
#166174=CARTESIAN_POINT('Ctrl Pts',(-17.0373338866468,-20.2186718275902,
13.990668356381));
#166175=CARTESIAN_POINT('Ctrl Pts',(-17.0107219488226,-20.1816581811141,
13.9878630472437));
#166176=CARTESIAN_POINT('Ctrl Pts',(-17.0063290290687,-20.1754784445367,
13.9873985692915));
#166177=CARTESIAN_POINT('Ctrl Pts',(-16.9995632764417,-20.1658516225195,
13.9866811910579));
#166178=CARTESIAN_POINT('Ctrl Pts',(-16.9971673558746,-20.1624209501328,
13.9864267516327));
#166179=CARTESIAN_POINT('Ctrl Pts',(-16.992749885307,-20.1560555373117,
13.9859569241591));
#166180=CARTESIAN_POINT('Ctrl Pts',(-16.9907255906737,-20.1531228217541,
13.9857413531691));
#166181=CARTESIAN_POINT('Ctrl Pts',(-16.9861746963316,-20.1464939314966,
13.9852560878668));
#166182=CARTESIAN_POINT('Ctrl Pts',(-16.9836524181472,-20.1427948555794,
13.9849866876068));
#166183=CARTESIAN_POINT('Ctrl Pts',(-16.9762679474938,-20.1318909192387,
13.9841965535607));
#166184=CARTESIAN_POINT('Ctrl Pts',(-16.9714383023856,-20.1246639832771,
13.9836779675989));
#166185=CARTESIAN_POINT('Ctrl Pts',(-16.9376215326702,-20.073380662921,
13.9800323698311));
#166186=CARTESIAN_POINT('Ctrl Pts',(-16.9102424847078,-20.0282804945466,
13.9770044185946));
#166187=CARTESIAN_POINT('Ctrl Pts',(-16.8769283941964,-19.9684747513366,
13.973152481501));
#166188=CARTESIAN_POINT('Ctrl Pts',(-16.8694353012686,-19.9546636379199,
13.972273883515));
#166189=CARTESIAN_POINT('Ctrl Pts',(-16.7917531791569,-19.8075986866824,
13.963020402823));
#166190=CARTESIAN_POINT('Ctrl Pts',(-16.7358199237623,-19.6672985567803,
13.9550418741927));
#166191=CARTESIAN_POINT('Ctrl Pts',(-16.6786700562493,-19.4629751067554,
13.943302459916));
#166192=CARTESIAN_POINT('Ctrl Pts',(-16.6646856642338,-19.4030144864149,
13.9398482784423));
#166193=CARTESIAN_POINT('Ctrl Pts',(-16.6464811915163,-19.306025395074,
13.9341845511461));
#166194=CARTESIAN_POINT('Ctrl Pts',(-16.6405912302544,-19.2693456024298,
13.932025680234));
#166195=CARTESIAN_POINT('Ctrl Pts',(-16.6341955207937,-19.2215067079759,
13.9291805581188));
#166196=CARTESIAN_POINT('Ctrl Pts',(-16.6328085296784,-19.2104707226106,
13.9285222036378));
#166197=CARTESIAN_POINT('Ctrl Pts',(-16.6306942844003,-19.1925049069366,
13.9274469857476));
#166198=CARTESIAN_POINT('Ctrl Pts',(-16.6299141509969,-19.1855814242963,
13.9270317949479));
#166199=CARTESIAN_POINT('Ctrl Pts',(-16.6284796090807,-19.1722595076541,
13.9262312461332));
#166200=CARTESIAN_POINT('Ctrl Pts',(-16.6278201536842,-19.1658616862521,
13.9258460519744));
#166201=CARTESIAN_POINT('Ctrl Pts',(-16.6263769640699,-19.1512057928275,
13.9249619450536));
#166202=CARTESIAN_POINT('Ctrl Pts',(-16.625612595598,-19.1429459593165,
13.9244624281989));
#166203=CARTESIAN_POINT('Ctrl Pts',(-16.6237108599387,-19.1209900023121,
13.9231312261583));
#166204=CARTESIAN_POINT('Ctrl Pts',(-16.6226582994084,-19.107287104761,
13.9222968918674));
#166205=CARTESIAN_POINT('Ctrl Pts',(-16.6156492014754,-19.0027133894429,
13.9159018783798));
#166206=CARTESIAN_POINT('Ctrl Pts',(-16.6154289765755,-18.9115654345479,
13.9101616903506));
#166207=CARTESIAN_POINT('Ctrl Pts',(-16.6298062740627,-18.6802080758641,
13.8951896727587));
#166208=CARTESIAN_POINT('Ctrl Pts',(-16.652526716625,-18.540945083973,13.8857808166372));
#166209=CARTESIAN_POINT('Ctrl Pts',(-16.7027934891498,-18.3530150138238,
13.8730499831034));
#166210=CARTESIAN_POINT('Ctrl Pts',(-16.7186705068227,-18.3015918780689,
13.8695669561803));
#166211=CARTESIAN_POINT('Ctrl Pts',(-16.7457537754623,-18.224436830547,
13.8643941405357));
#166212=CARTESIAN_POINT('Ctrl Pts',(-16.7555396984852,-18.1982319813948,
13.8626469172767));
#166213=CARTESIAN_POINT('Ctrl Pts',(-16.7683850010594,-18.165810252608,
13.8605040155152));
#166214=CARTESIAN_POINT('Ctrl Pts',(-16.7709588260316,-18.1594055290996,
13.8600816261532));
#166215=CARTESIAN_POINT('Ctrl Pts',(-16.7750868929788,-18.1492766843221,
13.8594152380421));
#166216=CARTESIAN_POINT('Ctrl Pts',(-16.7766205105752,-18.1455442867704,
13.859170026412));
#166217=CARTESIAN_POINT('Ctrl Pts',(-16.7795369287051,-18.138503867484,
13.8587081715774));
#166218=CARTESIAN_POINT('Ctrl Pts',(-16.780917443828,-18.1351950149378,
13.8584914010853));
#166219=CARTESIAN_POINT('Ctrl Pts',(-16.7840980326324,-18.1276258694268,
13.8579961761178));
#166220=CARTESIAN_POINT('Ctrl Pts',(-16.7859036636946,-18.1233679616951,
13.8577180627045));
#166221=CARTESIAN_POINT('Ctrl Pts',(-16.790745127673,-18.1120544674999,
13.8569802592059));
#166222=CARTESIAN_POINT('Ctrl Pts',(-16.7938054622387,-18.105009353016,
13.8565220189608));
#166223=CARTESIAN_POINT('Ctrl Pts',(-16.8158172413755,-18.0550819824384,
13.8532820550441));
#166224=CARTESIAN_POINT('Ctrl Pts',(-16.8361517793974,-18.0128195729012,
13.8505788338361));
#166225=CARTESIAN_POINT('Ctrl Pts',(-16.8622548894907,-17.9628849218245,
13.8473921435814));
#166226=CARTESIAN_POINT('Ctrl Pts',(-16.8666912053126,-17.9545350802392,
13.8468595336313));
#166227=CARTESIAN_POINT('Ctrl Pts',(-16.9495543953602,-17.8010639600214,
13.8370697901186));
#166228=CARTESIAN_POINT('Ctrl Pts',(-17.0446244900916,-17.6655641278161,
13.8283772994982));
#166229=CARTESIAN_POINT('Ctrl Pts',(-17.1946818535298,-17.497408547478,
13.8158966267372));
#166230=CARTESIAN_POINT('Ctrl Pts',(-17.2368015447831,-17.4540905822883,
13.8125041463953));
#166231=CARTESIAN_POINT('Ctrl Pts',(-17.3073622529474,-17.387475507713,
13.8069324970062));
#166232=CARTESIAN_POINT('Ctrl Pts',(-17.3346589072069,-17.3630140289342,
13.804801877169));
#166233=CARTESIAN_POINT('Ctrl Pts',(-17.3710083433145,-17.3321033119606,
13.8019889058576));
#166234=CARTESIAN_POINT('Ctrl Pts',(-17.3794971322821,-17.3249986138849,
13.8013336602531));
#166235=CARTESIAN_POINT('Ctrl Pts',(-17.3934098967941,-17.3135386622874,
13.8002622589076));
#166236=CARTESIAN_POINT('Ctrl Pts',(-17.3988003747197,-17.309142934133,
13.7998477532396));
#166237=CARTESIAN_POINT('Ctrl Pts',(-17.4092198962982,-17.3007313682633,
13.7990476487931));
#166238=CARTESIAN_POINT('Ctrl Pts',(-17.4142457882592,-17.296711736133,
13.7986622091267));
#166239=CARTESIAN_POINT('Ctrl Pts',(-17.4258116925875,-17.2875476609736,
13.797776295505));
#166240=CARTESIAN_POINT('Ctrl Pts',(-17.432363832322,-17.2824187589559,
13.7972752091056));
#166241=CARTESIAN_POINT('Ctrl Pts',(-17.4498869072675,-17.2688678438976,
13.7959370948986));
#166242=CARTESIAN_POINT('Ctrl Pts',(-17.4609102893831,-17.2605145982584,
13.7950973741676));
#166243=CARTESIAN_POINT('Ctrl Pts',(-17.5478113223775,-17.1959938516101,
13.788492543134));
#166244=CARTESIAN_POINT('Ctrl Pts',(-17.6272770229325,-17.1448582822446,
13.7825340005772));
#166245=CARTESIAN_POINT('Ctrl Pts',(-17.8649989507245,-17.0134594411235,
13.7649613241975));
#166246=CARTESIAN_POINT('Ctrl Pts',(-18.030255929927,-16.9475448290306,
13.7529883196793));
#166247=CARTESIAN_POINT('Ctrl Pts',(-18.2409377359212,-16.892821776179,
13.73906029975));
#166248=CARTESIAN_POINT('Ctrl Pts',(-18.2803769179404,-16.8837756536014,
13.7365113679217));
#166249=CARTESIAN_POINT('Ctrl Pts',(-18.327620672732,-16.8743560521237,
13.733546088942));
#166250=CARTESIAN_POINT('Ctrl Pts',(-18.3351957454265,-16.8728887229116,
13.7330733130385));
#166251=CARTESIAN_POINT('Ctrl Pts',(-18.3469196367595,-16.8706841793789,
13.7323459155056));
#166252=CARTESIAN_POINT('Ctrl Pts',(-18.3510628270251,-16.8699178990631,
13.7320896865725));
#166253=CARTESIAN_POINT('Ctrl Pts',(-18.3587123022363,-16.8685267393389,
13.7316181854028));
#166254=CARTESIAN_POINT('Ctrl Pts',(-18.3622178500195,-16.8678983428661,
13.7314027197448));
#166255=CARTESIAN_POINT('Ctrl Pts',(-18.3700981299812,-16.8665062575944,
13.7309197259417));
#166256=CARTESIAN_POINT('Ctrl Pts',(-18.3744736751895,-16.8657474881474,
13.7306524795444));
#166257=CARTESIAN_POINT('Ctrl Pts',(-18.3856620565777,-16.8638435397812,
13.7299714429248));
#166258=CARTESIAN_POINT('Ctrl Pts',(-18.3924782298691,-16.862717920271,
13.729558737507));
#166259=CARTESIAN_POINT('Ctrl Pts',(-18.4320757636264,-16.8563777646128,
13.7271732821514));
#166260=CARTESIAN_POINT('Ctrl Pts',(-18.4649725959688,-16.8519011144175,
13.7252395420557));
#166261=CARTESIAN_POINT('Ctrl Pts',(-18.5165060387728,-16.8461192945068,
13.722266216998));
#166262=CARTESIAN_POINT('Ctrl Pts',(-18.5350761803347,-16.8442840513349,
13.7212060535681));
#166263=CARTESIAN_POINT('Ctrl Pts',(-18.5848200668732,-16.8400312853727,
13.718390684282));
#166264=CARTESIAN_POINT('Ctrl Pts',(-18.616027717275,-16.838058379965,13.7166500582021));
#166265=CARTESIAN_POINT('Ctrl Pts',(-18.68572842501,-16.835200410613,13.712798128199));
#166266=CARTESIAN_POINT('Ctrl Pts',(-18.7242249885063,-16.8346726223255,
13.710694808877));
#166267=CARTESIAN_POINT('Ctrl Pts',(-18.8719904178439,-16.8366771173393,
13.7026494073521));
#166268=CARTESIAN_POINT('Ctrl Pts',(-18.9809856286892,-16.8466189272732,
13.6967644777885));
#166269=CARTESIAN_POINT('Ctrl Pts',(-19.1429758994154,-16.874151050549,
13.6876274890093));
#166270=CARTESIAN_POINT('Ctrl Pts',(-19.1968465613857,-16.8854836171478,
13.6845241836493));
#166271=CARTESIAN_POINT('Ctrl Pts',(-19.2834498582769,-16.9072583411936,
13.6793865221568));
#166272=CARTESIAN_POINT('Ctrl Pts',(-19.3164784167342,-16.9164208941806,
13.6773914262923));
#166273=CARTESIAN_POINT('Ctrl Pts',(-19.3596071847738,-16.9295209777438,
13.6747330844915));
#166274=CARTESIAN_POINT('Ctrl Pts',(-19.369921314309,-16.9327402790717,
13.6740933148737));
#166275=CARTESIAN_POINT('Ctrl Pts',(-19.3867783029255,-16.9381437340827,
13.6730408982627));
#166276=CARTESIAN_POINT('Ctrl Pts',(-19.3933360114689,-16.9402811839638,
13.6726297908862));
#166277=CARTESIAN_POINT('Ctrl Pts',(-19.4060125483478,-16.9444816737608,
13.6718317521141));
#166278=CARTESIAN_POINT('Ctrl Pts',(-19.4121326201157,-16.9465407400236,
13.6714449557201));
#166279=CARTESIAN_POINT('Ctrl Pts',(-19.4262461222219,-16.9513611456157,
13.6705494206052));
#166280=CARTESIAN_POINT('Ctrl Pts',(-19.4342325775575,-16.9541424341338,
13.670040025033));
#166281=CARTESIAN_POINT('Ctrl Pts',(-19.4556758312295,-16.9617544338049,
13.6686651159863));
#166282=CARTESIAN_POINT('Ctrl Pts',(-19.4691005306975,-16.9666736758996,
13.6677966704614));
#166283=CARTESIAN_POINT('Ctrl Pts',(-19.592328958455,-17.0132497568144,
13.6597527510237));
#166284=CARTESIAN_POINT('Ctrl Pts',(-19.6985201378396,-17.0638331403191,
13.6522722846333));
#166285=CARTESIAN_POINT('Ctrl Pts',(-19.9414515472103,-17.2054117586762,
13.6339020390175));
#166286=CARTESIAN_POINT('Ctrl Pts',(-20.072896412781,-17.3040113998141,
13.6228710079268));
#166287=CARTESIAN_POINT('Ctrl Pts',(-20.2141769117082,-17.4381541448046,
13.6105089692731));
#166288=CARTESIAN_POINT('Ctrl Pts',(-20.2362207830319,-17.4600261670342,
13.6085650322808));
#166289=CARTESIAN_POINT('Ctrl Pts',(-20.2627314468167,-17.4875137068112,
13.6062172177954));
#166290=CARTESIAN_POINT('Ctrl Pts',(-20.2676601593797,-17.4926760269561,
13.6057802891099));
#166291=CARTESIAN_POINT('Ctrl Pts',(-20.2753701286764,-17.5008336308648,
13.6050962575892));
#166292=CARTESIAN_POINT('Ctrl Pts',(-20.2781689266112,-17.5038121560977,
13.6048478328276));
#166293=CARTESIAN_POINT('Ctrl Pts',(-20.2833998779188,-17.5094114233512,
13.6043833447437));
#166294=CARTESIAN_POINT('Ctrl Pts',(-20.2858339899481,-17.5120301909328,
13.6041671343974));
#166295=CARTESIAN_POINT('Ctrl Pts',(-20.2913956841174,-17.5180442851251,
13.6036729353168));
#166296=CARTESIAN_POINT('Ctrl Pts',(-20.2945187977089,-17.5214436774273,
13.6033952874689));
#166297=CARTESIAN_POINT('Ctrl Pts',(-20.304155013997,-17.5320014459726,
13.6025380966028));
#166298=CARTESIAN_POINT('Ctrl Pts',(-20.3106302734806,-17.5391944046701,
13.6019613457059));
#166299=CARTESIAN_POINT('Ctrl Pts',(-20.3791745620288,-17.6163941059099,
13.5958449039933));
#166300=CARTESIAN_POINT('Ctrl Pts',(-20.4365950923684,-17.6904070118395,
13.5906201463139));
#166301=CARTESIAN_POINT('Ctrl Pts',(-20.5627799908811,-17.877437094088,
13.5782429302421));
#166302=CARTESIAN_POINT('Ctrl Pts',(-20.6262222119337,-17.993554852825,
13.5711935662999));
#166303=CARTESIAN_POINT('Ctrl Pts',(-20.6941947372831,-18.1514291345996,
13.5616457581666));
#166304=CARTESIAN_POINT('Ctrl Pts',(-20.708915345871,-18.1884649857798,
13.5594101580691));
#166305=CARTESIAN_POINT('Ctrl Pts',(-20.7225805759573,-18.2258896138153,
13.5571445817067));
#166306=CARTESIAN_POINT('',(-20.8509992001584,-18.9500893141201,14.0892704168218));
#166307=CARTESIAN_POINT('Ctrl Pts',(-20.7225805383928,-18.2258895109384,
13.3344632701429));
#166308=CARTESIAN_POINT('Ctrl Pts',(-20.7140997256968,-18.2026633224573,
13.3360898678322));
#166309=CARTESIAN_POINT('Ctrl Pts',(-20.7052099499586,-18.1795801024561,
13.3377116603475));
#166310=CARTESIAN_POINT('Ctrl Pts',(-20.6896738686132,-18.1412567374251,
13.3404079591312));
#166311=CARTESIAN_POINT('Ctrl Pts',(-20.683252173486,-18.1259365018981,
13.3414868503263));
#166312=CARTESIAN_POINT('Ctrl Pts',(-20.6554928164708,-18.0618377305783,
13.3460009999898));
#166313=CARTESIAN_POINT('Ctrl Pts',(-20.632497437654,-18.0137931890523,
13.3493852384935));
#166314=CARTESIAN_POINT('Ctrl Pts',(-20.6036571232171,-17.9589505700114,
13.3532075704532));
#166315=CARTESIAN_POINT('Ctrl Pts',(-20.5995537513667,-17.9512632036568,
13.3537423864081));
#166316=CARTESIAN_POINT('Ctrl Pts',(-20.5932681151595,-17.9396605497492,
13.3545478723295));
#166317=CARTESIAN_POINT('Ctrl Pts',(-20.5911207479857,-17.9357266042847,
13.3548206754776));
#166318=CARTESIAN_POINT('Ctrl Pts',(-20.5872434452906,-17.9286767698784,
13.3553089697548));
#166319=CARTESIAN_POINT('Ctrl Pts',(-20.58551812815,-17.9255584173787,13.3555247485522));
#166320=CARTESIAN_POINT('Ctrl Pts',(-20.5817516591871,-17.9187912673803,
13.3559925534721));
#166321=CARTESIAN_POINT('Ctrl Pts',(-20.5797075772965,-17.9151441667258,
13.3562443882116));
#166322=CARTESIAN_POINT('Ctrl Pts',(-20.5739344574349,-17.9049147964847,
13.356949999503));
#166323=CARTESIAN_POINT('Ctrl Pts',(-20.5701808785337,-17.8983463489839,
13.3574022278542));
#166324=CARTESIAN_POINT('Ctrl Pts',(-20.5475081236854,-17.8591600627494,
13.3600958701374));
#166325=CARTESIAN_POINT('Ctrl Pts',(-20.527754170794,-17.8270301275868,
13.3622866718655));
#166326=CARTESIAN_POINT('Ctrl Pts',(-20.4598647486886,-17.7229468928424,
13.3693824410159));
#166327=CARTESIAN_POINT('Ctrl Pts',(-20.4081729372359,-17.6534130691412,
13.3741229837252));
#166328=CARTESIAN_POINT('Ctrl Pts',(-20.2388248844504,-17.4525968152739,
13.388417610194));
#166329=CARTESIAN_POINT('Ctrl Pts',(-20.1089424673344,-17.3326685377626,
13.3978831132822));
#166330=CARTESIAN_POINT('Ctrl Pts',(-19.9470527295094,-17.2168577587889,
13.409450069178));
#166331=CARTESIAN_POINT('Ctrl Pts',(-19.9281750522112,-17.2038119649424,
13.4107944175979));
#166332=CARTESIAN_POINT('Ctrl Pts',(-19.9011552309914,-17.1857812551975,
13.4127141111369));
#166333=CARTESIAN_POINT('Ctrl Pts',(-19.8931852908434,-17.1805403067843,
13.4132798108868));
#166334=CARTESIAN_POINT('Ctrl Pts',(-19.8801738731756,-17.1721095427535,
13.4142025867968));
#166335=CARTESIAN_POINT('Ctrl Pts',(-19.875153795802,-17.1688868234034,
13.4145584298995));
#166336=CARTESIAN_POINT('Ctrl Pts',(-19.8646137410571,-17.1621832063159,
13.4153052021165));
#166337=CARTESIAN_POINT('Ctrl Pts',(-19.8590911632111,-17.1587065328271,
13.4156962828169));
#166338=CARTESIAN_POINT('Ctrl Pts',(-19.8459085946077,-17.150492466,13.4166293783693));
#166339=CARTESIAN_POINT('Ctrl Pts',(-19.8382343195216,-17.1457783409854,
13.4171722429262));
#166340=CARTESIAN_POINT('Ctrl Pts',(-19.8122484043422,-17.1300433176869,
13.4190094454509));
#166341=CARTESIAN_POINT('Ctrl Pts',(-19.7938004833726,-17.1192510655922,
13.4203120739224));
#166342=CARTESIAN_POINT('Ctrl Pts',(-19.6922725130606,-17.0619014722255,
13.4274744994076));
#166343=CARTESIAN_POINT('Ctrl Pts',(-19.6062972601117,-17.0207175467903,
13.4335233267607));
#166344=CARTESIAN_POINT('Ctrl Pts',(-19.3593949823414,-16.9223034938732,
13.4507948383493));
#166345=CARTESIAN_POINT('Ctrl Pts',(-19.1938957496031,-16.8785295908205,
13.4623043893491));
#166346=CARTESIAN_POINT('Ctrl Pts',(-18.9884991558451,-16.85003118873,13.4755393953443));
#166347=CARTESIAN_POINT('Ctrl Pts',(-18.9519273095244,-16.8459252698673,
13.4778537801019));
#166348=CARTESIAN_POINT('Ctrl Pts',(-18.9081486791395,-16.842162980718,
13.48055961979));
#166349=CARTESIAN_POINT('Ctrl Pts',(-18.9010295875812,-16.8415874501487,
13.4809975956011));
#166350=CARTESIAN_POINT('Ctrl Pts',(-18.8894080893929,-16.8407071052158,
13.4817090940777));
#166351=CARTESIAN_POINT('Ctrl Pts',(-18.8849074472827,-16.8403806439035,
13.4819837863723));
#166352=CARTESIAN_POINT('Ctrl Pts',(-18.8768483173873,-16.8398219595999,
13.4824741064647));
#166353=CARTESIAN_POINT('Ctrl Pts',(-18.8732902681027,-16.8395843358969,
13.482690032465));
#166354=CARTESIAN_POINT('Ctrl Pts',(-18.8655823031331,-16.8390891204712,
13.483156612986));
#166355=CARTESIAN_POINT('Ctrl Pts',(-18.861432237046,-16.8388347643941,
13.4834070844442));
#166356=CARTESIAN_POINT('Ctrl Pts',(-18.8498346670885,-16.8381582432594,
13.4841050351879));
#166357=CARTESIAN_POINT('Ctrl Pts',(-18.8423855569119,-16.8377632068639,
13.4845510198406));
#166358=CARTESIAN_POINT('Ctrl Pts',(-18.7990585884251,-16.8356951104398,
13.4871324249199));
#166359=CARTESIAN_POINT('Ctrl Pts',(-18.7631425826237,-16.8348958313183,
13.4892220156317));
#166360=CARTESIAN_POINT('Ctrl Pts',(-18.6474945266842,-16.8352661414381,
13.4958379844384));
#166361=CARTESIAN_POINT('Ctrl Pts',(-18.5678392824195,-16.8400250888151,
13.5002243290217));
#166362=CARTESIAN_POINT('Ctrl Pts',(-18.3036786030416,-16.8708493772849,
13.5147244717422));
#166363=CARTESIAN_POINT('Ctrl Pts',(-18.1223976098282,-16.9167356492839,
13.5246809892134));
#166364=CARTESIAN_POINT('Ctrl Pts',(-17.9289806596003,-16.9939093609115,
13.536793282158));
#166365=CARTESIAN_POINT('Ctrl Pts',(-17.9086325759213,-17.00239910476,13.5380857651937));
#166366=CARTESIAN_POINT('Ctrl Pts',(-17.8806750307968,-17.014579835793,
13.5398884657194));
#166367=CARTESIAN_POINT('Ctrl Pts',(-17.872949080915,-17.0180011097885,
13.540389504952));
#166368=CARTESIAN_POINT('Ctrl Pts',(-17.8597034874644,-17.0239617429605,
13.5412535359755));
#166369=CARTESIAN_POINT('Ctrl Pts',(-17.8541738747296,-17.0264787976894,
13.5416157596264));
#166370=CARTESIAN_POINT('Ctrl Pts',(-17.8427959661267,-17.0317172140661,
13.5423642541021));
#166371=CARTESIAN_POINT('Ctrl Pts',(-17.8369491255737,-17.0344415692843,
13.5427506253296));
#166372=CARTESIAN_POINT('Ctrl Pts',(-17.8233709213203,-17.0408440714321,
13.543651996248));
#166373=CARTESIAN_POINT('Ctrl Pts',(-17.8156492787915,-17.0445424639774,
13.5441676942268));
#166374=CARTESIAN_POINT('Ctrl Pts',(-17.7910017922441,-17.0565320876256,
13.545823899905));
#166375=CARTESIAN_POINT('Ctrl Pts',(-17.7741645187312,-17.0650023742698,
13.5469706326529));
#166376=CARTESIAN_POINT('Ctrl Pts',(-17.6906014235813,-17.1084480205814,
13.552740523411));
#166377=CARTESIAN_POINT('Ctrl Pts',(-17.6256697793026,-17.1467392315843,
13.557480085036));
#166378=CARTESIAN_POINT('Ctrl Pts',(-17.4719788015028,-17.2487944783576,
13.5693359018199));
#166379=CARTESIAN_POINT('Ctrl Pts',(-17.3858489648803,-17.3161235165715,
13.5765519881518));
#166380=CARTESIAN_POINT('Ctrl Pts',(-17.2943894784147,-17.3997663762781,
13.5847394763276));
#166381=CARTESIAN_POINT('Ctrl Pts',(-17.2835818943926,-17.4098602531417,
13.5857158257668));
#166382=CARTESIAN_POINT('Ctrl Pts',(-17.1976226427082,-17.491845998022,
13.5935486530659));
#166383=CARTESIAN_POINT('Ctrl Pts',(-17.1277466129228,-17.5690826875177,
13.6003416506233));
#166384=CARTESIAN_POINT('Ctrl Pts',(-17.057872973444,-17.6587942808735,
13.6073672271781));
#166385=CARTESIAN_POINT('Ctrl Pts',(-17.051972828847,-17.666477754054,13.6079624323683));
#166386=CARTESIAN_POINT('Ctrl Pts',(-17.0433381408901,-17.6778835202656,
13.608836086388));
#166387=CARTESIAN_POINT('Ctrl Pts',(-17.0405627996145,-17.681574569263,
13.6091172961327));
#166388=CARTESIAN_POINT('Ctrl Pts',(-17.0356600964017,-17.6881395029313,
13.6096147313358));
#166389=CARTESIAN_POINT('Ctrl Pts',(-17.0335279172941,-17.6910097221541,
13.6098312911786));
#166390=CARTESIAN_POINT('Ctrl Pts',(-17.0289747128538,-17.6971715394593,
13.610294224304));
#166391=CARTESIAN_POINT('Ctrl Pts',(-17.0265559489038,-17.7004647395233,
13.6105404410541));
#166392=CARTESIAN_POINT('Ctrl Pts',(-17.0199414904071,-17.7095253356414,
13.6112146353298));
#166393=CARTESIAN_POINT('Ctrl Pts',(-17.0157653378792,-17.7153070247375,
13.6116412789131));
#166394=CARTESIAN_POINT('Ctrl Pts',(-16.9936078185478,-17.7463119862559,
13.6139108475841));
#166395=CARTESIAN_POINT('Ctrl Pts',(-16.9761514530323,-17.7719079502791,
13.6157199200887));
#166396=CARTESIAN_POINT('Ctrl Pts',(-16.8701129766784,-17.9349675839643,
13.6269072190229));
#166397=CARTESIAN_POINT('Ctrl Pts',(-16.7971380216548,-18.0819380516337,
13.6355501683147));
#166398=CARTESIAN_POINT('Ctrl Pts',(-16.7019803899064,-18.3466517233322,
13.6509452032218));
#166399=CARTESIAN_POINT('Ctrl Pts',(-16.6714699089154,-18.4605587446626,
13.6575148200393));
#166400=CARTESIAN_POINT('Ctrl Pts',(-16.6480483140075,-18.5904767082956,
13.6652484282959));
#166401=CARTESIAN_POINT('Ctrl Pts',(-16.6456537143955,-18.6045761908023,
13.6660905974197));
#166402=CARTESIAN_POINT('Ctrl Pts',(-16.6420705639612,-18.6270511232341,
13.6674380376078));
#166403=CARTESIAN_POINT('Ctrl Pts',(-16.6407890146802,-18.6354114568612,
13.6679403615201));
#166404=CARTESIAN_POINT('Ctrl Pts',(-16.6386174640658,-18.6501677191829,
13.6688289991286));
#166405=CARTESIAN_POINT('Ctrl Pts',(-16.6377065577357,-18.6565604966579,
13.669214645714));
#166406=CARTESIAN_POINT('Ctrl Pts',(-16.6358832671285,-18.6697895436354,
13.6700141118039));
#166407=CARTESIAN_POINT('Ctrl Pts',(-16.6349750148609,-18.6766262967393,
13.670428057106));
#166408=CARTESIAN_POINT('Ctrl Pts',(-16.6327298982582,-18.6941828921962,
13.6714931194885));
#166409=CARTESIAN_POINT('Ctrl Pts',(-16.6314416628657,-18.7049086530796,
13.67214576359));
#166410=CARTESIAN_POINT('Ctrl Pts',(-16.6264111340294,-18.7496844652818,
13.6748788036134));
#166411=CARTESIAN_POINT('Ctrl Pts',(-16.6234136393663,-18.7838114079327,
13.6769824664931));
#166412=CARTESIAN_POINT('Ctrl Pts',(-16.6177643956782,-18.8728784215353,
13.6825295580915));
#166413=CARTESIAN_POINT('Ctrl Pts',(-16.6164234538964,-18.9278729967481,
13.6860112451016));
#166414=CARTESIAN_POINT('Ctrl Pts',(-16.6188178731786,-19.0921455464016,
13.6965704085244));
#166415=CARTESIAN_POINT('Ctrl Pts',(-16.6288727173682,-19.2011422472975,
13.7037963099291));
#166416=CARTESIAN_POINT('Ctrl Pts',(-16.6537814520219,-19.3467913599842,
13.7135573676062));
#166417=CARTESIAN_POINT('Ctrl Pts',(-16.661300308591,-19.3845338322806,
13.7160951787984));
#166418=CARTESIAN_POINT('Ctrl Pts',(-16.6768194325393,-19.4526836670681,
13.7206740430664));
#166419=CARTESIAN_POINT('Ctrl Pts',(-16.684476396842,-19.4831583106033,
13.7227202264793));
#166420=CARTESIAN_POINT('Ctrl Pts',(-16.7060867296695,-19.5617238918079,
13.7279748925652));
#166421=CARTESIAN_POINT('Ctrl Pts',(-16.7210737955619,-19.6095138226699,
13.7311511391529));
#166422=CARTESIAN_POINT('Ctrl Pts',(-16.7403469552473,-19.6641079525071,
13.7347216404907));
#166423=CARTESIAN_POINT('Ctrl Pts',(-16.7429920707199,-19.6714703807263,
13.7352019041542));
#166424=CARTESIAN_POINT('Ctrl Pts',(-16.7472801112778,-19.6832009710555,
13.7359649258532));
#166425=CARTESIAN_POINT('Ctrl Pts',(-16.7488967439463,-19.687578575057,
13.7362491812701));
#166426=CARTESIAN_POINT('Ctrl Pts',(-16.751782949525,-19.6953151813461,
13.7367506401667));
#166427=CARTESIAN_POINT('Ctrl Pts',(-16.7530466100361,-19.6986763432342,
13.7369681921469));
#166428=CARTESIAN_POINT('Ctrl Pts',(-16.7557401372558,-19.7057857844427,
13.7374276888843));
#166429=CARTESIAN_POINT('Ctrl Pts',(-16.7571721049696,-19.7095332120891,
13.7376695057031));
#166430=CARTESIAN_POINT('Ctrl Pts',(-16.7610588300651,-19.7196186129533,
13.7383193191846));
#166431=CARTESIAN_POINT('Ctrl Pts',(-16.763533495767,-19.725948934708,13.7387261384488));
#166432=CARTESIAN_POINT('Ctrl Pts',(-16.7758761031225,-19.7570790019163,
13.7407220475595));
#166433=CARTESIAN_POINT('Ctrl Pts',(-16.786182434969,-19.7817037289964,
13.7422862252088));
#166434=CARTESIAN_POINT('Ctrl Pts',(-16.8171977959429,-19.8520423900543,
13.7467298369642));
#166435=CARTESIAN_POINT('Ctrl Pts',(-16.8390708079562,-19.8972253809776,
13.7495542946331));
#166436=CARTESIAN_POINT('Ctrl Pts',(-16.9239141563581,-20.0576772663545,
13.75962114507));
#166437=CARTESIAN_POINT('Ctrl Pts',(-16.9959669729675,-20.1678028703928,
13.7666181239493));
#166438=CARTESIAN_POINT('Ctrl Pts',(-17.1431422403223,-20.3526712097384,
13.7796117497776));
#166439=CARTESIAN_POINT('Ctrl Pts',(-17.2145324694088,-20.4298100472926,
13.7855061735589));
#166440=CARTESIAN_POINT('Ctrl Pts',(-17.3016464824971,-20.5109261136325,
13.7924814135577));
#166441=CARTESIAN_POINT('Ctrl Pts',(-17.3120457229041,-20.5204174337361,
13.7933106888672));
#166442=CARTESIAN_POINT('Ctrl Pts',(-17.3287943748239,-20.535400329009,
13.7946413429502));
#166443=CARTESIAN_POINT('Ctrl Pts',(-17.3350832267281,-20.5409591905696,
13.7951398896436));
#166444=CARTESIAN_POINT('Ctrl Pts',(-17.3462606078872,-20.5507213461684,
13.7960241368025));
#166445=CARTESIAN_POINT('Ctrl Pts',(-17.3511356189083,-20.5549400067391,
13.7964091912981));
#166446=CARTESIAN_POINT('Ctrl Pts',(-17.3612859311094,-20.5636429574033,
13.7972096990382));
#166447=CARTESIAN_POINT('Ctrl Pts',(-17.3665641072611,-20.5681237621406,
13.7976252892904));
#166448=CARTESIAN_POINT('Ctrl Pts',(-17.3802271697713,-20.5796079000919,
13.7986994085144));
#166449=CARTESIAN_POINT('Ctrl Pts',(-17.3886443803018,-20.5865722993634,
13.7993595149462));
#166450=CARTESIAN_POINT('Ctrl Pts',(-17.4245097909862,-20.6157826391659,
13.8021657360717));
#166451=CARTESIAN_POINT('Ctrl Pts',(-17.4524574314345,-20.6374037162345,
13.8043367044642));
#166452=CARTESIAN_POINT('Ctrl Pts',(-17.5271912972352,-20.6922861205314,
13.8101050116233));
#166453=CARTESIAN_POINT('Ctrl Pts',(-17.5748096560177,-20.7243599670701,
13.8137445222459));
#166454=CARTESIAN_POINT('Ctrl Pts',(-17.7245790189376,-20.8166193140851,
13.8250717711392));
#166455=CARTESIAN_POINT('Ctrl Pts',(-17.8305251155659,-20.8701931868951,
13.8329351818468));
#166456=CARTESIAN_POINT('Ctrl Pts',(-18.0381718596145,-20.9541582639182,
13.8477080786132));
#166457=CARTESIAN_POINT('Ctrl Pts',(-18.1387881851723,-20.9863408508938,
13.854602481805));
#166458=CARTESIAN_POINT('Ctrl Pts',(-18.2508144784688,-21.0131439931278,
13.8617192156344));
#166459=CARTESIAN_POINT('Ctrl Pts',(-18.260249668403,-21.0153330899585,
13.8623143164452));
#166460=CARTESIAN_POINT('Ctrl Pts',(-18.2742049855909,-21.0184701467707,
13.8631878470701));
#166461=CARTESIAN_POINT('Ctrl Pts',(-18.2787135688655,-21.0194681592053,
13.8634690366977));
#166462=CARTESIAN_POINT('Ctrl Pts',(-18.2867189020335,-21.021212749662,
13.8639664496666));
#166463=CARTESIAN_POINT('Ctrl Pts',(-18.2902143102526,-21.0219652282625,
13.864183007281));
#166464=CARTESIAN_POINT('Ctrl Pts',(-18.2977085174992,-21.0235586979776,
13.864645950415));
#166465=CARTESIAN_POINT('Ctrl Pts',(-18.3017078387464,-21.0243969660365,
13.8648921793249));
#166466=CARTESIAN_POINT('Ctrl Pts',(-18.3126950647206,-21.0266667276134,
13.8655664412073));
#166467=CARTESIAN_POINT('Ctrl Pts',(-18.3196878905484,-21.028074506952,
13.8659931397916));
#166468=CARTESIAN_POINT('Ctrl Pts',(-18.357098027051,-21.0354092813369,
13.8682635270551));
#166469=CARTESIAN_POINT('Ctrl Pts',(-18.3876373215015,-21.0407035342838,
13.8700733342172));
#166470=CARTESIAN_POINT('Ctrl Pts',(-18.5800207910995,-21.0697189021429,
13.8812635286908));
#166471=CARTESIAN_POINT('Ctrl Pts',(-18.7440573512384,-21.0752885214934,
13.8899084050625));
#166472=CARTESIAN_POINT('Ctrl Pts',(-19.0243994562741,-21.052287063675,
13.9053029776013));
#166473=CARTESIAN_POINT('Ctrl Pts',(-19.1406631071423,-21.0329030176184,
13.911869773093));
#166474=CARTESIAN_POINT('Ctrl Pts',(-19.2685672101117,-21.0004460955248,
13.9196002060546));
#166475=CARTESIAN_POINT('Ctrl Pts',(-19.2823922637549,-20.9967883554316,
13.9204423379327));
#166476=CARTESIAN_POINT('Ctrl Pts',(-19.3043331006423,-20.9907448808141,
13.921789729658));
#166477=CARTESIAN_POINT('Ctrl Pts',(-19.3124736254387,-20.9884500475678,
13.9222920426886));
#166478=CARTESIAN_POINT('Ctrl Pts',(-19.3268045873397,-20.9843172534022,
13.923180667619));
#166479=CARTESIAN_POINT('Ctrl Pts',(-19.3330008107649,-20.9824996243596,
13.9235663124689));
#166480=CARTESIAN_POINT('Ctrl Pts',(-19.3457976655777,-20.9786820628479,
13.9243657814118));
#166481=CARTESIAN_POINT('Ctrl Pts',(-19.3523970261013,-20.9766781679649,
13.9247797313342));
#166482=CARTESIAN_POINT('Ctrl Pts',(-19.369308094027,-20.9714527314666,
13.9258448191825));
#166483=CARTESIAN_POINT('Ctrl Pts',(-19.3796050536432,-20.9681844699579,
13.9264974842708));
#166484=CARTESIAN_POINT('Ctrl Pts',(-19.421801582802,-20.9544348719619,
13.9291894395693));
#166485=CARTESIAN_POINT('Ctrl Pts',(-19.4534732108165,-20.9432745992925,
13.9312509841543));
#166486=CARTESIAN_POINT('Ctrl Pts',(-19.5351606113183,-20.9122868117059,
13.9366788028705));
#166487=CARTESIAN_POINT('Ctrl Pts',(-19.5847073637069,-20.8912985648005,
13.940081644078));
#166488=CARTESIAN_POINT('Ctrl Pts',(-19.7590211255306,-20.8094922872943,
13.9524453325196));
#166489=CARTESIAN_POINT('Ctrl Pts',(-19.8785357599393,-20.7383307517078,
13.9616908974154));
#166490=CARTESIAN_POINT('Ctrl Pts',(-20.0633780619625,-20.6020621379154,
13.9767881809416));
#166491=CARTESIAN_POINT('Ctrl Pts',(-20.1330007581972,-20.5434621715121,
13.9826868325319));
#166492=CARTESIAN_POINT('Ctrl Pts',(-20.2056220821844,-20.4738773840299,
13.9889006167982));
#166493=CARTESIAN_POINT('Ctrl Pts',(-20.2125516650544,-20.4671459687698,
13.9894941620132));
#166494=CARTESIAN_POINT('Ctrl Pts',(-20.2227217037495,-20.4571305480552,
13.9903658533879));
#166495=CARTESIAN_POINT('Ctrl Pts',(-20.2259977809915,-20.4538831180721,
13.9906467429663));
#166496=CARTESIAN_POINT('Ctrl Pts',(-20.2317939704682,-20.448099930615,
13.9911438244957));
#166497=CARTESIAN_POINT('Ctrl Pts',(-20.2343182970572,-20.4455684746767,
13.9913603490581));
#166498=CARTESIAN_POINT('Ctrl Pts',(-20.2397163708351,-20.4401276600474,
13.9918234423276));
#166499=CARTESIAN_POINT('Ctrl Pts',(-20.24258809648,-20.4372163740709,13.99206985327));
#166500=CARTESIAN_POINT('Ctrl Pts',(-20.2484649752047,-20.431223905618,
13.9925742727638));
#166501=CARTESIAN_POINT('Ctrl Pts',(-20.2514692059129,-20.4281418407161,
13.9928322099775));
#166502=CARTESIAN_POINT('Ctrl Pts',(-20.2652664701271,-20.4139004805739,
13.9940173096999));
#166503=CARTESIAN_POINT('Ctrl Pts',(-20.2759462702773,-20.4026315000053,
13.9949360391927));
#166504=CARTESIAN_POINT('Ctrl Pts',(-20.3410495727756,-20.3324051484403,
14.0005529595109));
#166505=CARTESIAN_POINT('Ctrl Pts',(-20.3922144945842,-20.2705045048262,
14.0050403501236));
#166506=CARTESIAN_POINT('Ctrl Pts',(-20.4809416628919,-20.1497987291867,
14.0132760841966));
#166507=CARTESIAN_POINT('Ctrl Pts',(-20.5193512764045,-20.0917579492557,
14.0170382609235));
#166508=CARTESIAN_POINT('Ctrl Pts',(-20.6313102103813,-19.9029877845586,
14.0289663785397));
#166509=CARTESIAN_POINT('Ctrl Pts',(-20.6938625764002,-19.7663059930405,
14.0371981153533));
#166510=CARTESIAN_POINT('Ctrl Pts',(-20.745951996354,-19.6107403493133,
14.0468105577194));
#166511=CARTESIAN_POINT('Ctrl Pts',(-20.7503149306902,-19.5972625583361,
14.0476448853232));
#166512=CARTESIAN_POINT('Ctrl Pts',(-20.7570544852589,-19.5757070035014,
14.0489821190155));
#166513=CARTESIAN_POINT('Ctrl Pts',(-20.7595187964723,-19.5676569487601,
14.0494821481899));
#166514=CARTESIAN_POINT('Ctrl Pts',(-20.7637864757215,-19.5534129017074,
14.0503681159981));
#166515=CARTESIAN_POINT('Ctrl Pts',(-20.7656096812489,-19.5472249297501,
14.0507534003742));
#166516=CARTESIAN_POINT('Ctrl Pts',(-20.7693280076272,-19.5343887795456,
14.0515534868461));
#166517=CARTESIAN_POINT('Ctrl Pts',(-20.7712189019553,-19.5277394661866,
14.0519684215081));
#166518=CARTESIAN_POINT('Ctrl Pts',(-20.7760008784298,-19.5106051428325,
14.0530389334059));
#166519=CARTESIAN_POINT('Ctrl Pts',(-20.7788437611398,-19.5001069956869,
14.0536960679433));
#166520=CARTESIAN_POINT('Ctrl Pts',(-20.7848190503623,-19.4773478463147,
14.0551235064335));
#166521=CARTESIAN_POINT('Ctrl Pts',(-20.7879226529658,-19.4650797810014,
14.0558947147319));
#166522=CARTESIAN_POINT('Ctrl Pts',(-20.7966336980483,-19.4293001665496,
14.0581493044168));
#166523=CARTESIAN_POINT('Ctrl Pts',(-20.8019485533546,-19.4057200974013,
14.0596419062654));
#166524=CARTESIAN_POINT('Ctrl Pts',(-20.8363441713581,-19.2399337326738,
14.0701853145707));
#166525=CARTESIAN_POINT('Ctrl Pts',(-20.8511300498368,-19.0951834122695,
14.0796830572144));
#166526=CARTESIAN_POINT('Ctrl Pts',(-20.8509991383111,-18.9500899240172,
14.0892704847094));
#166527=CARTESIAN_POINT('Ctrl Pts',(-20.8509991377672,-18.9500893212942,
14.0892705245358));
#166528=CARTESIAN_POINT('Ctrl Pts',(-20.8508884780097,-18.8274802136491,
14.0973722384938));
#166529=CARTESIAN_POINT('Ctrl Pts',(-20.8401264223167,-18.7050980350981,
14.1054939319305));
#166530=CARTESIAN_POINT('Ctrl Pts',(-20.8166444854234,-18.5719488868771,
14.1139585516479));
#166531=CARTESIAN_POINT('Ctrl Pts',(-20.8143518751223,-18.5595933316814,
14.1147402926256));
#166532=CARTESIAN_POINT('Ctrl Pts',(-20.8106712434454,-18.5406969048476,
14.115929398801));
#166533=CARTESIAN_POINT('Ctrl Pts',(-20.8093620674484,-18.5341411947832,
14.1163407347543));
#166534=CARTESIAN_POINT('Ctrl Pts',(-20.8071513237826,-18.5233376109753,
14.1170164988066));
#166535=CARTESIAN_POINT('Ctrl Pts',(-20.8062677119474,-18.5190861681048,
14.1172818880159));
#166536=CARTESIAN_POINT('Ctrl Pts',(-20.8045210241027,-18.5108099824553,
14.1177974250332));
#166537=CARTESIAN_POINT('Ctrl Pts',(-20.8036592788867,-18.5067849813663,
14.1180476457386));
#166538=CARTESIAN_POINT('Ctrl Pts',(-20.8020280137088,-18.4992728345161,
14.1185136771087));
#166539=CARTESIAN_POINT('Ctrl Pts',(-20.8012614184,-18.4957851601687,14.1187296456484));
#166540=CARTESIAN_POINT('Ctrl Pts',(-20.7994932703445,-18.4878368284238,
14.119220944986));
#166541=CARTESIAN_POINT('Ctrl Pts',(-20.7984860931811,-18.483377474242,
14.1194959498741));
#166542=CARTESIAN_POINT('Ctrl Pts',(-20.7953527021747,-18.4697103149334,
14.1203369411167));
#166543=CARTESIAN_POINT('Ctrl Pts',(-20.7931792404185,-18.4605133100409,
14.1209002854826));
#166544=CARTESIAN_POINT('Ctrl Pts',(-20.7723521633478,-18.3749475295864,
14.1261199678598));
#166545=CARTESIAN_POINT('Ctrl Pts',(-20.7495260400938,-18.299684482012,
14.1305523345105));
#166546=CARTESIAN_POINT('Ctrl Pts',(-20.7225805482453,-18.2258895379212,
14.1348940720942));
#166547=CARTESIAN_POINT('Origin',(-18.734,-18.952,0.));
#166548=CARTESIAN_POINT('',(-20.7225805737622,-18.2258896078036,15.1555945473776));
#166549=CARTESIAN_POINT('',(-20.7225805503655,-18.2258895437275,14.9318514930297));
#166550=CARTESIAN_POINT('',(-20.7225805737622,-18.2258896078036,0.));
#166551=CARTESIAN_POINT('',(-20.8523539179813,-18.9502594238256,15.1109429533473));
#166552=CARTESIAN_POINT('Ctrl Pts',(-20.8509992748742,-18.9502478064743,
15.1109437209775));
#166553=CARTESIAN_POINT('Ctrl Pts',(-20.8509006165464,-18.8310488678702,
15.1181312937192));
#166554=CARTESIAN_POINT('Ctrl Pts',(-20.8407310772906,-18.7122546433193,
15.1253188664609));
#166555=CARTESIAN_POINT('Ctrl Pts',(-20.8207141748805,-18.5951905938,15.1325064392026));
#166556=CARTESIAN_POINT('Ctrl Pts',(-20.8084963315187,-18.5237374692842,
15.1368935634494));
#166557=CARTESIAN_POINT('Ctrl Pts',(-20.7925803619145,-18.4527731734038,
15.1412806876962));
#166558=CARTESIAN_POINT('Ctrl Pts',(-20.7730188005911,-18.3827098008609,
15.1456678119431));
#166559=CARTESIAN_POINT('Ctrl Pts',(-20.7582648347418,-18.3298657262649,
15.1489767237546));
#166560=CARTESIAN_POINT('Ctrl Pts',(-20.7414380855554,-18.277534208989,
15.1522856355661));
#166561=CARTESIAN_POINT('Ctrl Pts',(-20.7225805737622,-18.2258896078036,
15.1555945473776));
#166562=CARTESIAN_POINT('Ctrl Pts',(-20.7249097977618,-18.2250590878524,
14.355439975907));
#166563=CARTESIAN_POINT('Ctrl Pts',(-20.6989344912625,-18.1521456629184,
14.360110516976));
#166564=CARTESIAN_POINT('Ctrl Pts',(-20.3954318177898,-17.4332648257454,
14.4071729936054));
#166565=CARTESIAN_POINT('Ctrl Pts',(-19.0148744663066,-16.4645435790994,
14.4966274057954));
#166566=CARTESIAN_POINT('Ctrl Pts',(-16.7944748199427,-17.3694160408942,
14.6238032124768));
#166567=CARTESIAN_POINT('Ctrl Pts',(-16.3534691457724,-19.7262110589277,
14.7509790191583));
#166568=CARTESIAN_POINT('Ctrl Pts',(-18.0964527779473,-21.3727154833541,
14.8781548258396));
#166569=CARTESIAN_POINT('Ctrl Pts',(-20.2927765759232,-20.8308253929522,
14.9981428039027));
#166570=CARTESIAN_POINT('Ctrl Pts',(-20.8471439650915,-19.534463852321,
15.0757388464053));
#166571=CARTESIAN_POINT('Ctrl Pts',(-20.8523539179813,-18.9502594238256,
15.1109429533473));
#166572=CARTESIAN_POINT('Ctrl Pts',(-20.7225805482453,-18.2258895379212,
14.1348940720942));
#166573=CARTESIAN_POINT('Ctrl Pts',(-20.707502733624,-18.1845963044093,
14.1373235662296));
#166574=CARTESIAN_POINT('Ctrl Pts',(-20.6911350897703,-18.1437627423971,
14.1397244927296));
#166575=CARTESIAN_POINT('Ctrl Pts',(-20.6449227773403,-18.0381371044714,
14.1459967299859));
#166576=CARTESIAN_POINT('Ctrl Pts',(-20.6130671130522,-17.9743099162901,
14.1498507562372));
#166577=CARTESIAN_POINT('Ctrl Pts',(-20.5342706048791,-17.8345651178331,
14.1586406107144));
#166578=CARTESIAN_POINT('Ctrl Pts',(-20.4856320614129,-17.7597677103411,
14.1635989258829));
#166579=CARTESIAN_POINT('Ctrl Pts',(-20.4120582786952,-17.6608866196624,
14.1706898593858));
#166580=CARTESIAN_POINT('Ctrl Pts',(-20.3910309374818,-17.6340084877275,
14.1726761120272));
#166581=CARTESIAN_POINT('Ctrl Pts',(-20.3624525439932,-17.5992436398234,
14.1753299557445));
#166582=CARTESIAN_POINT('Ctrl Pts',(-20.3554763928526,-17.5908895126539,
14.1759743426739));
#166583=CARTESIAN_POINT('Ctrl Pts',(-20.3439634012343,-17.5773165241001,
14.1770324207133));
#166584=CARTESIAN_POINT('Ctrl Pts',(-20.3394648061884,-17.5720653759787,
14.1774445395521));
#166585=CARTESIAN_POINT('Ctrl Pts',(-20.3307201063842,-17.561958450634,
14.1782431677588));
#166586=CARTESIAN_POINT('Ctrl Pts',(-20.3264773709349,-17.5570998499078,
14.1786295348415));
#166587=CARTESIAN_POINT('Ctrl Pts',(-20.316648725643,-17.5459477887591,
14.1795220849354));
#166588=CARTESIAN_POINT('Ctrl Pts',(-20.3110473916266,-17.5396681229666,
14.1800289110287));
#166589=CARTESIAN_POINT('Ctrl Pts',(-20.2959253366837,-17.5229168888778,
14.1813924050948));
#166590=CARTESIAN_POINT('Ctrl Pts',(-20.2863369245266,-17.512507258319,
14.1822519298717));
#166591=CARTESIAN_POINT('Ctrl Pts',(-20.2021839445793,-17.4229654550481,
14.1897536291562));
#166592=CARTESIAN_POINT('Ctrl Pts',(-20.1217415373617,-17.3496024822226,
14.1966553495631));
#166593=CARTESIAN_POINT('Ctrl Pts',(-19.9590042495324,-17.2226657405498,
14.2100939977286));
#166594=CARTESIAN_POINT('Ctrl Pts',(-19.8779113499631,-17.1679882900035,
14.2165787219792));
#166595=CARTESIAN_POINT('Ctrl Pts',(-19.7310865022736,-17.0831294331119,
14.2277562426462));
#166596=CARTESIAN_POINT('Ctrl Pts',(-19.66703816724,-17.0503428538897,14.2324611436209));
#166597=CARTESIAN_POINT('Ctrl Pts',(-19.570731222272,-17.0070827054999,
14.2391772890039));
#166598=CARTESIAN_POINT('Ctrl Pts',(-19.5396941270583,-16.9940215296004,
14.241289168206));
#166599=CARTESIAN_POINT('Ctrl Pts',(-19.5015759896546,-16.9790405019908,
14.243808284867));
#166600=CARTESIAN_POINT('Ctrl Pts',(-19.4947814012484,-16.9764105325894,
14.244254473837));
#166601=CARTESIAN_POINT('Ctrl Pts',(-19.4840930400149,-16.9723367269592,
14.2449517481225));
#166602=CARTESIAN_POINT('Ctrl Pts',(-19.4802084401077,-16.9708692097942,
14.2452042145345));
#166603=CARTESIAN_POINT('Ctrl Pts',(-19.472979405025,-16.9681625169269,
14.2456722388445));
#166604=CARTESIAN_POINT('Ctrl Pts',(-19.4696361888589,-16.9669203748444,
14.2458879680286));
#166605=CARTESIAN_POINT('Ctrl Pts',(-19.4620491211678,-16.9641232672844,
14.2463759290164));
#166606=CARTESIAN_POINT('Ctrl Pts',(-19.4578034301438,-16.9625734437562,
14.2466478524034));
#166607=CARTESIAN_POINT('Ctrl Pts',(-19.4451918054621,-16.958015483434,
14.2474523079116));
#166608=CARTESIAN_POINT('Ctrl Pts',(-19.4368117305669,-16.9550463916004,
14.2479825740317));
#166609=CARTESIAN_POINT('Ctrl Pts',(-19.3737813934032,-16.9331604238273,
14.2519407069241));
#166610=CARTESIAN_POINT('Ctrl Pts',(-19.3183900465949,-16.9164354574461,
14.2552492223628));
#166611=CARTESIAN_POINT('Ctrl Pts',(-19.1043468997635,-16.8612668298124,
14.2676350961639));
#166612=CARTESIAN_POINT('Ctrl Pts',(-18.9421302667622,-16.8389429270101,
14.276240860935));
#166613=CARTESIAN_POINT('Ctrl Pts',(-18.7188998916316,-16.8342019031165,
14.2886086156895));
#166614=CARTESIAN_POINT('Ctrl Pts',(-18.658825349921,-16.835482869544,14.291983310044));
#166615=CARTESIAN_POINT('Ctrl Pts',(-18.5747475981794,-16.8408598127308,
14.2968212630423));
#166616=CARTESIAN_POINT('Ctrl Pts',(-18.550634613922,-16.8428173892078,
14.2982219233524));
#166617=CARTESIAN_POINT('Ctrl Pts',(-18.5085797231295,-16.8469581560757,
14.3006907659365));
#166618=CARTESIAN_POINT('Ctrl Pts',(-18.4906221402878,-16.8489587133596,
14.3017532747122));
#166619=CARTESIAN_POINT('Ctrl Pts',(-18.4642216584597,-16.8522425101154,
14.3033284126285));
#166620=CARTESIAN_POINT('Ctrl Pts',(-18.4557570975741,-16.8533473956169,
14.303835420355));
#166621=CARTESIAN_POINT('Ctrl Pts',(-18.4409124051437,-16.8553764716857,
14.3047281587992));
#166622=CARTESIAN_POINT('Ctrl Pts',(-18.4345293426919,-16.8562786726924,
14.3051131896441));
#166623=CARTESIAN_POINT('Ctrl Pts',(-18.4221313181258,-16.8580888440937,
14.305863346691));
#166624=CARTESIAN_POINT('Ctrl Pts',(-18.4161159470959,-16.8589936141352,
14.3062283679213));
#166625=CARTESIAN_POINT('Ctrl Pts',(-18.4017264520659,-16.8612213973453,
14.3071041035565));
#166626=CARTESIAN_POINT('Ctrl Pts',(-18.3933562611894,-16.8625688056523,
14.3076155877192));
#166627=CARTESIAN_POINT('Ctrl Pts',(-18.3630693681826,-16.8676311250196,
14.3094740220012));
#166628=CARTESIAN_POINT('Ctrl Pts',(-18.3412040226162,-16.8716407998544,
14.310830291111));
#166629=CARTESIAN_POINT('Ctrl Pts',(-18.1386086613959,-16.9121005653244,
14.3235370765305));
#166630=CARTESIAN_POINT('Ctrl Pts',(-17.9633343551751,-16.9716646897236,
14.3356748925132));
#166631=CARTESIAN_POINT('Ctrl Pts',(-17.7254086641247,-17.0889412809956,
14.3531899125361));
#166632=CARTESIAN_POINT('Ctrl Pts',(-17.6548952835398,-17.1288765738331,
14.3585115566974));
#166633=CARTESIAN_POINT('Ctrl Pts',(-17.5563731920112,-17.1923983100319,
14.3659856297798));
#166634=CARTESIAN_POINT('Ctrl Pts',(-17.5264146902734,-17.2128217198054,
14.3682634042163));
#166635=CARTESIAN_POINT('Ctrl Pts',(-17.4909237354192,-17.2383762537897,
14.3709540780363));
#166636=CARTESIAN_POINT('Ctrl Pts',(-17.4848770368072,-17.2427788996733,
14.3714122151689));
#166637=CARTESIAN_POINT('Ctrl Pts',(-17.4755019515319,-17.2496812913505,
14.3721219291204));
#166638=CARTESIAN_POINT('Ctrl Pts',(-17.4721574585316,-17.2521589118258,
14.3723749938538));
#166639=CARTESIAN_POINT('Ctrl Pts',(-17.4659614929848,-17.2567772836794,
14.3728435600627));
#166640=CARTESIAN_POINT('Ctrl Pts',(-17.463108148362,-17.2589153550628,
14.373059236371));
#166641=CARTESIAN_POINT('Ctrl Pts',(-17.4566606449759,-17.2637720887509,
14.3735463575713));
#166642=CARTESIAN_POINT('Ctrl Pts',(-17.4530697665441,-17.2664950174813,
14.3738174984965));
#166643=CARTESIAN_POINT('Ctrl Pts',(-17.4422365027572,-17.2747643930803,
14.3746351159321));
#166644=CARTESIAN_POINT('Ctrl Pts',(-17.4350211370524,-17.2803462875632,
14.3751791596857));
#166645=CARTESIAN_POINT('Ctrl Pts',(-17.3795390550491,-17.3238440493634,
14.3793604568176));
#166646=CARTESIAN_POINT('Ctrl Pts',(-17.3329010200042,-17.363799953952,
14.3828631914692));
#166647=CARTESIAN_POINT('Ctrl Pts',(-17.1808057771431,-17.5060263520505,
14.3945000839994));
#166648=CARTESIAN_POINT('Ctrl Pts',(-17.0842725629316,-17.6172131127653,
14.4022866534614));
#166649=CARTESIAN_POINT('Ctrl Pts',(-16.9468074857225,-17.8134764928882,
14.4154841570817));
#166650=CARTESIAN_POINT('Ctrl Pts',(-16.8986502333391,-17.8928582654723,
14.420692585604));
#166651=CARTESIAN_POINT('Ctrl Pts',(-16.8461311090808,-17.9938328974515,
14.4273222610451));
#166652=CARTESIAN_POINT('Ctrl Pts',(-16.8366864196515,-18.0126734985682,
14.4285591422182));
#166653=CARTESIAN_POINT('Ctrl Pts',(-16.8236312642079,-18.0397168730359,
14.4303356725141));
#166654=CARTESIAN_POINT('Ctrl Pts',(-16.8197889710002,-18.0478067998837,
14.4308672557061));
#166655=CARTESIAN_POINT('Ctrl Pts',(-16.8132397964634,-18.061824900431,
14.4317887200009));
#166656=CARTESIAN_POINT('Ctrl Pts',(-16.8105087221281,-18.0677416837436,
14.4321777585026));
#166657=CARTESIAN_POINT('Ctrl Pts',(-16.8053255545808,-18.0791084841885,
14.4329253857192));
#166658=CARTESIAN_POINT('Ctrl Pts',(-16.8028691315946,-18.0845564671159,
14.433283820683));
#166659=CARTESIAN_POINT('Ctrl Pts',(-16.7965280034257,-18.0987805829214,
14.434219968693));
#166660=CARTESIAN_POINT('Ctrl Pts',(-16.7926798845747,-18.1075727882821,
14.4347989285279));
#166661=CARTESIAN_POINT('Ctrl Pts',(-16.7796940626519,-18.1378008277755,
14.4367906526954));
#166662=CARTESIAN_POINT('Ctrl Pts',(-16.7708508182644,-18.1593606047104,
14.4382133600276));
#166663=CARTESIAN_POINT('Ctrl Pts',(-16.7001127360201,-18.3402694669195,
14.4501732455666));
#166664=CARTESIAN_POINT('Ctrl Pts',(-16.6573841189443,-18.5064033231155,
14.4613736928985));
#166665=CARTESIAN_POINT('Ctrl Pts',(-16.6233203227714,-18.7652862150299,
14.4786285618332));
#166666=CARTESIAN_POINT('Ctrl Pts',(-16.617279953992,-18.85541336513,14.4845834405331));
#166667=CARTESIAN_POINT('Ctrl Pts',(-16.6168937485584,-18.9842815274449,
14.4928167545805));
#166668=CARTESIAN_POINT('Ctrl Pts',(-16.6178351419536,-19.0229063125209,
14.4952477332147));
#166669=CARTESIAN_POINT('Ctrl Pts',(-16.6202270208638,-19.0690931745979,
14.4980939507509));
#166670=CARTESIAN_POINT('Ctrl Pts',(-16.6206620134154,-19.0766979445322,
14.4985606097976));
#166671=CARTESIAN_POINT('Ctrl Pts',(-16.6214000296449,-19.0884842067556,
14.4992806227628));
#166672=CARTESIAN_POINT('Ctrl Pts',(-16.6216744391971,-19.0926673356527,
14.499535533618));
#166673=CARTESIAN_POINT('Ctrl Pts',(-16.6222050590464,-19.10040425159,14.5000057986263));
#166674=CARTESIAN_POINT('Ctrl Pts',(-16.6224578130785,-19.1039581774259,
14.5002213384898));
#166675=CARTESIAN_POINT('Ctrl Pts',(-16.6230477081639,-19.1119668051106,
14.5007059900314));
#166676=CARTESIAN_POINT('Ctrl Pts',(-16.6233899772391,-19.1164210747067,
14.5009748109626));
#166677=CARTESIAN_POINT('Ctrl Pts',(-16.6244360979845,-19.1294934040059,
14.5017616734413));
#166678=CARTESIAN_POINT('Ctrl Pts',(-16.6251786617099,-19.1381083934463,
14.5022775937213));
#166679=CARTESIAN_POINT('Ctrl Pts',(-16.6307248635287,-19.1981515951569,
14.5058564298033));
#166680=CARTESIAN_POINT('Ctrl Pts',(-16.6373568970773,-19.2493979500217,
14.5088243661345));
#166681=CARTESIAN_POINT('Ctrl Pts',(-16.6494414417739,-19.321836351759,
14.512960364339));
#166682=CARTESIAN_POINT('Ctrl Pts',(-16.653356506915,-19.3432620728162,
14.5141762324835));
#166683=CARTESIAN_POINT('Ctrl Pts',(-16.6665993301805,-19.4099023400314,
14.5179447529216));
#166684=CARTESIAN_POINT('Ctrl Pts',(-16.6770759599669,-19.4548755528155,
14.5204691381087));
#166685=CARTESIAN_POINT('Ctrl Pts',(-16.7172948679962,-19.6051063544682,
14.5289363881225));
#166686=CARTESIAN_POINT('Ctrl Pts',(-16.7537170859711,-19.7083902412168,
14.5348247302892));
#166687=CARTESIAN_POINT('Ctrl Pts',(-16.8202493131744,-19.8587993779259,
14.543969652374));
#166688=CARTESIAN_POINT('Ctrl Pts',(-16.8445041725424,-19.9083114950661,
14.5470775046067));
#166689=CARTESIAN_POINT('Ctrl Pts',(-16.8869471269055,-19.987017821485,
14.5522220220363));
#166690=CARTESIAN_POINT('Ctrl Pts',(-16.9039633466278,-20.0168154100458,
14.5542192894047));
#166691=CARTESIAN_POINT('Ctrl Pts',(-16.9272822665565,-20.055438657677,
14.5568801143203));
#166692=CARTESIAN_POINT('Ctrl Pts',(-16.9329397995333,-20.0646490854403,
14.5575201395267));
#166693=CARTESIAN_POINT('Ctrl Pts',(-16.9423229784206,-20.0796657466327,
14.5585728694591));
#166694=CARTESIAN_POINT('Ctrl Pts',(-16.9460069531642,-20.0854978820092,
14.5589840327675));
#166695=CARTESIAN_POINT('Ctrl Pts',(-16.9531942099514,-20.0967538724314,
14.5597821035472));
#166696=CARTESIAN_POINT('Ctrl Pts',(-16.9566939348884,-20.1021799162748,
14.5601688756115));
#166697=CARTESIAN_POINT('Ctrl Pts',(-16.9648334161859,-20.1146736765535,
14.5610642428417));
#166698=CARTESIAN_POINT('Ctrl Pts',(-16.9694907751497,-20.1217297429807,
14.5615734940843));
#166699=CARTESIAN_POINT('Ctrl Pts',(-16.9821331246805,-20.1406360406638,
14.5629477610436));
#166700=CARTESIAN_POINT('Ctrl Pts',(-16.9901959298311,-20.152433478021,
14.5638157045524));
#166701=CARTESIAN_POINT('Ctrl Pts',(-17.0652574980544,-20.2599108955587,
14.5718202909221));
#166702=CARTESIAN_POINT('Ctrl Pts',(-17.1399371257419,-20.3499585840822,
14.5792584768438));
#166703=CARTESIAN_POINT('Ctrl Pts',(-17.3354199611098,-20.5495286040024,
14.597505795565));
#166704=CARTESIAN_POINT('Ctrl Pts',(-17.4621895115106,-20.6521829016177,
14.6084546437164));
#166705=CARTESIAN_POINT('Ctrl Pts',(-17.627039443414,-20.7568253765623,
14.620863629073));
#166706=CARTESIAN_POINT('Ctrl Pts',(-17.655024909666,-20.7736940853253,
14.6229114564933));
#166707=CARTESIAN_POINT('Ctrl Pts',(-17.6896861172972,-20.7935075580639,
14.625366588211));
#166708=CARTESIAN_POINT('Ctrl Pts',(-17.6959994465687,-20.7970735558757,
14.6258105453715));
#166709=CARTESIAN_POINT('Ctrl Pts',(-17.7059218432776,-20.8026110377434,
14.6265030956947));
#166710=CARTESIAN_POINT('Ctrl Pts',(-17.7095184764235,-20.8046045227902,
14.6267530648796));
#166711=CARTESIAN_POINT('Ctrl Pts',(-17.7162497605517,-20.8083098356687,
14.6272188772913));
#166712=CARTESIAN_POINT('Ctrl Pts',(-17.7193829006355,-20.8100241919327,
14.6274348768802));
#166713=CARTESIAN_POINT('Ctrl Pts',(-17.7265418205627,-20.8139178209395,
14.627926569461));
#166714=CARTESIAN_POINT('Ctrl Pts',(-17.7305703318085,-20.8160919658492,
14.6282019345012));
#166715=CARTESIAN_POINT('Ctrl Pts',(-17.7429638509639,-20.822728798854,
14.6290451229149));
#166716=CARTESIAN_POINT('Ctrl Pts',(-17.7513519434513,-20.827148445346,
14.6296102841839));
#166717=CARTESIAN_POINT('Ctrl Pts',(-17.8671859292204,-20.8871900981783,
14.6373429986399));
#166718=CARTESIAN_POINT('Ctrl Pts',(-17.9791944290598,-20.9335661655134,
14.6439805057908));
#166719=CARTESIAN_POINT('Ctrl Pts',(-18.2651924255875,-21.0241835095277,
14.6603064593958));
#166720=CARTESIAN_POINT('Ctrl Pts',(-18.4419637514492,-21.0563841948392,
14.6699251402767));
#166721=CARTESIAN_POINT('Ctrl Pts',(-18.642123633161,-21.0671144549188,
14.6815960955469));
#166722=CARTESIAN_POINT('Ctrl Pts',(-18.6635892682765,-21.0679377833667,
14.6828564502759));
#166723=CARTESIAN_POINT('Ctrl Pts',(-18.6940855940363,-21.068642928833,
14.6846608395756));
#166724=CARTESIAN_POINT('Ctrl Pts',(-18.7031091692341,-21.0687938493666,
14.685196452973));
#166725=CARTESIAN_POINT('Ctrl Pts',(-18.7186621460312,-21.068954505945,
14.6861226874363));
#166726=CARTESIAN_POINT('Ctrl Pts',(-18.7251911832734,-21.0689917414294,
14.6865124420484));
#166727=CARTESIAN_POINT('Ctrl Pts',(-18.7376819738936,-21.0690051925942,
14.6872599007969));
#166728=CARTESIAN_POINT('Ctrl Pts',(-18.7436436678334,-21.0689864290881,
14.6876174437478));
#166729=CARTESIAN_POINT('Ctrl Pts',(-18.7591228075927,-21.0688723237722,
14.6885478696725));
#166730=CARTESIAN_POINT('Ctrl Pts',(-18.768639753568,-21.0687379794059,
14.6891219695787));
#166731=CARTESIAN_POINT('Ctrl Pts',(-18.8009696859958,-21.0680635107694,
14.691079382418));
#166732=CARTESIAN_POINT('Ctrl Pts',(-18.8237740980564,-21.0672187281264,
14.6924721817665));
#166733=CARTESIAN_POINT('Ctrl Pts',(-19.0240757280663,-21.0565537154634,
14.7048164834835));
#166734=CARTESIAN_POINT('Ctrl Pts',(-19.1996626289566,-21.0247817669645,
14.7164925311726));
#166735=CARTESIAN_POINT('Ctrl Pts',(-19.4506665101214,-20.9458344943402,
14.7338754759693));
#166736=CARTESIAN_POINT('Ctrl Pts',(-19.5305375663184,-20.9152923006605,
14.7395017807799));
#166737=CARTESIAN_POINT('Ctrl Pts',(-19.6424270586408,-20.864550511978,
14.7473429782496));
#166738=CARTESIAN_POINT('Ctrl Pts',(-19.6760922432131,-20.848194026208,
14.7496961010084));
#166739=CARTESIAN_POINT('Ctrl Pts',(-19.7160080828495,-20.8274749012922,
14.7524634050521));
#166740=CARTESIAN_POINT('Ctrl Pts',(-19.7226892732827,-20.8239614058514,
14.7529258188324));
#166741=CARTESIAN_POINT('Ctrl Pts',(-19.7330383414801,-20.8184481887533,
14.7536407028168));
#166742=CARTESIAN_POINT('Ctrl Pts',(-19.7367192564565,-20.8164732613998,
14.7538946954068));
#166743=CARTESIAN_POINT('Ctrl Pts',(-19.7435300021399,-20.8127930776969,
14.7543641105007));
#166744=CARTESIAN_POINT('Ctrl Pts',(-19.7466613443232,-20.8110908275909,
14.7545797133162));
#166745=CARTESIAN_POINT('Ctrl Pts',(-19.7537247501403,-20.8072279004783,
14.7550655709126));
#166746=CARTESIAN_POINT('Ctrl Pts',(-19.7576542420374,-20.8050626331488,
14.7553355284645));
#166747=CARTESIAN_POINT('Ctrl Pts',(-19.7692143287784,-20.7986446879429,
14.7561288154487));
#166748=CARTESIAN_POINT('Ctrl Pts',(-19.7768256261236,-20.7943571937778,
14.7566499713084));
#166749=CARTESIAN_POINT('Ctrl Pts',(-19.8310962478148,-20.7633421127041,
14.7603592573306));
#166750=CARTESIAN_POINT('Ctrl Pts',(-19.8767530185861,-20.7348900713738,
14.7634443584259));
#166751=CARTESIAN_POINT('Ctrl Pts',(-20.0608279562891,-20.6101995162181,
14.7759434364569));
#166752=CARTESIAN_POINT('Ctrl Pts',(-20.1885934080942,-20.499340890524,
14.7848133067536));
#166753=CARTESIAN_POINT('Ctrl Pts',(-20.3564534647442,-20.3143266674313,
14.7986576872988));
#166754=CARTESIAN_POINT('Ctrl Pts',(-20.4075288571257,-20.2510720812714,
14.8032487951523));
#166755=CARTESIAN_POINT('Ctrl Pts',(-20.4662740102747,-20.1690871364965,
14.8091326478384));
#166756=CARTESIAN_POINT('Ctrl Pts',(-20.4774847986288,-20.1529725488644,
14.810285933835));
#166757=CARTESIAN_POINT('Ctrl Pts',(-20.4933402542996,-20.129491665318,
14.8119628819907));
#166758=CARTESIAN_POINT('Ctrl Pts',(-20.4981663215216,-20.1222486653921,
14.812479681482));
#166759=CARTESIAN_POINT('Ctrl Pts',(-20.5065035600957,-20.1095672900544,
14.8133837821075));
#166760=CARTESIAN_POINT('Ctrl Pts',(-20.5100347292345,-20.1041421529798,
14.813770327022));
#166761=CARTESIAN_POINT('Ctrl Pts',(-20.5168105239017,-20.093626940683,
14.8145191342108));
#166762=CARTESIAN_POINT('Ctrl Pts',(-20.5200583734894,-20.0885390099521,
14.8148812712892));
#166763=CARTESIAN_POINT('Ctrl Pts',(-20.5277198381499,-20.0764229703323,
14.8157432390812));
#166764=CARTESIAN_POINT('Ctrl Pts',(-20.5321139486244,-20.0693827001873,
14.8162437856645));
#166765=CARTESIAN_POINT('Ctrl Pts',(-20.5475456049671,-20.0443312533415,
14.818023883128));
#166766=CARTESIAN_POINT('Ctrl Pts',(-20.5583545593534,-20.0261813717135,
14.8193117641296));
#166767=CARTESIAN_POINT('Ctrl Pts',(-20.6657650088142,-19.839524182704,
14.8325424137311));
#166768=CARTESIAN_POINT('Ctrl Pts',(-20.7389930443321,-19.6586728277574,
14.8453728959637));
#166769=CARTESIAN_POINT('Ctrl Pts',(-20.8048202355923,-19.398055353222,
14.8631017541084));
#166770=CARTESIAN_POINT('Ctrl Pts',(-20.8192617767641,-19.3247555236717,
14.8679935204894));
#166771=CARTESIAN_POINT('Ctrl Pts',(-20.8346727919646,-19.2166767560843,
14.8749433752754));
#166772=CARTESIAN_POINT('Ctrl Pts',(-20.8387085640078,-19.1823956212695,
14.8771093266513));
#166773=CARTESIAN_POINT('Ctrl Pts',(-20.8425871759834,-19.1406888050124,
14.8796857842226));
#166774=CARTESIAN_POINT('Ctrl Pts',(-20.843231456135,-19.1333450081682,
14.880137248492));
#166775=CARTESIAN_POINT('Ctrl Pts',(-20.844177533657,-19.121873202885,14.880838889526));
#166776=CARTESIAN_POINT('Ctrl Pts',(-20.8445056015823,-19.1177475036803,
14.8810905010912));
#166777=CARTESIAN_POINT('Ctrl Pts',(-20.8450939760934,-19.1100631376055,
14.8815577589508));
#166778=CARTESIAN_POINT('Ctrl Pts',(-20.8453573821213,-19.1065048108827,
14.8817735714453));
#166779=CARTESIAN_POINT('Ctrl Pts',(-20.8459354331482,-19.0984183338005,
14.8822627676358));
#166780=CARTESIAN_POINT('Ctrl Pts',(-20.8462445116755,-19.0938898376823,
14.8825358364075));
#166781=CARTESIAN_POINT('Ctrl Pts',(-20.8470081048128,-19.0821461249705,
14.8832417692837));
#166782=CARTESIAN_POINT('Ctrl Pts',(-20.8474402334159,-19.0749294432504,
14.8836734093755));
#166783=CARTESIAN_POINT('Ctrl Pts',(-20.8499256633027,-19.0295248659026,
14.8863762934984));
#166784=CARTESIAN_POINT('Ctrl Pts',(-20.8509809805955,-18.9912868194502,
14.8885955342883));
#166785=CARTESIAN_POINT('Ctrl Pts',(-20.8510792902781,-18.7909008209396,
14.9000236869547));
#166786=CARTESIAN_POINT('Ctrl Pts',(-20.832532273869,-18.6292767121341,
14.9085853292683));
#166787=CARTESIAN_POINT('Ctrl Pts',(-20.7763041393555,-18.3880942468308,
14.9221736104699));
#166788=CARTESIAN_POINT('Ctrl Pts',(-20.7518790836572,-18.3061287042505,
14.9269355922798));
#166789=CARTESIAN_POINT('Ctrl Pts',(-20.7225805503655,-18.2258895437275,
14.9318514930297));
#166790=CARTESIAN_POINT('Origin',(-18.734,-18.952,0.));
#166791=CARTESIAN_POINT('',(-20.7225805738037,-18.2258896079172,15.9575279467182));
#166792=CARTESIAN_POINT('',(-20.7225805680845,-18.2258895922541,15.7328935628168));
#166793=CARTESIAN_POINT('',(-20.7225805737622,-18.2258896078036,0.));
#166794=CARTESIAN_POINT('',(-20.8509995343428,-18.9534041339616,15.9109437209775));
#166795=CARTESIAN_POINT('Ctrl Pts',(-20.7225805738037,-18.2258896079172,
15.9575279467182));
#166796=CARTESIAN_POINT('Ctrl Pts',(-20.7279981079307,-18.2407264746532,
15.9565690253348));
#166797=CARTESIAN_POINT('Ctrl Pts',(-20.7332493642926,-18.2556233409562,
15.9556045828014));
#166798=CARTESIAN_POINT('Ctrl Pts',(-20.768347076402,-18.3588595979594,
15.9489085458843));
#166799=CARTESIAN_POINT('Ctrl Pts',(-20.7924915060708,-18.4490166027167,
15.9429916617944));
#166800=CARTESIAN_POINT('Ctrl Pts',(-20.8375614450588,-18.676438452644,
15.927941103698));
#166801=CARTESIAN_POINT('Ctrl Pts',(-20.8510859073874,-18.8147188131726,
15.918664814329));
#166802=CARTESIAN_POINT('Ctrl Pts',(-20.8509995894475,-18.9533184382234,
15.9096292174278));
#166803=CARTESIAN_POINT('Ctrl Pts',(-20.7225805737622,-18.2258896078036,
15.1555945473776));
#166804=CARTESIAN_POINT('Ctrl Pts',(-20.6976334619431,-18.1575675696285,
15.1599719962089));
#166805=CARTESIAN_POINT('Ctrl Pts',(-20.6691305109114,-18.090448506577,
15.1643494450402));
#166806=CARTESIAN_POINT('Ctrl Pts',(-20.6372132212172,-18.0249247956158,
15.1687268938715));
#166807=CARTESIAN_POINT('Ctrl Pts',(-20.6053187551123,-17.9594479397066,
15.1731012124529));
#166808=CARTESIAN_POINT('Ctrl Pts',(-20.5700150048519,-17.8955646048789,
15.1774755310343));
#166809=CARTESIAN_POINT('Ctrl Pts',(-20.5314915042865,-17.8336470628564,
15.1818498496157));
#166810=CARTESIAN_POINT('Ctrl Pts',(-20.4929828430108,-17.7717533715308,
15.1862224832053));
#166811=CARTESIAN_POINT('Ctrl Pts',(-20.4512571477743,-17.7118243791939,
15.1905951167949));
#166812=CARTESIAN_POINT('Ctrl Pts',(-20.4065489800678,-17.6542061376034,
15.1949677503846));
#166813=CARTESIAN_POINT('Ctrl Pts',(-20.3618432858589,-17.5965910837656,
15.1993401420565));
#166814=CARTESIAN_POINT('Ctrl Pts',(-20.3141557437213,-17.5412869069951,
15.2037125337283));
#166815=CARTESIAN_POINT('Ctrl Pts',(-20.2637621434272,-17.4886077817151,
15.2080849254002));
#166816=CARTESIAN_POINT('Ctrl Pts',(-20.2133188587134,-17.4358767186541,
15.2124616279319));
#166817=CARTESIAN_POINT('Ctrl Pts',(-20.1601645203762,-17.3857762266896,
15.2168383304635));
#166818=CARTESIAN_POINT('Ctrl Pts',(-20.104612302126,-17.3385840842298,
15.2212150329952));
#166819=CARTESIAN_POINT('Ctrl Pts',(-20.0490337746074,-17.2913695917939,
15.2255938083125));
#166820=CARTESIAN_POINT('Ctrl Pts',(-19.991055488614,-17.2470664862988,
15.2299725836298));
#166821=CARTESIAN_POINT('Ctrl Pts',(-19.9310221067214,-17.2059109197924,
15.2343513589471));
#166822=CARTESIAN_POINT('Ctrl Pts',(-19.8708775583487,-17.1646791436952,
15.2387382426372));
#166823=CARTESIAN_POINT('Ctrl Pts',(-19.8086707226497,-17.1266068052155,
15.2431251263273));
#166824=CARTESIAN_POINT('Ctrl Pts',(-19.7447731738505,-17.0918853285283,
15.2475120100174));
#166825=CARTESIAN_POINT('Ctrl Pts',(-19.6856842856162,-17.0597768440269,
15.2515687553062));
#166826=CARTESIAN_POINT('Ctrl Pts',(-19.6251501220134,-17.0305334662485,
15.2556255005951));
#166827=CARTESIAN_POINT('Ctrl Pts',(-19.5634785608967,-17.0042694444527,
15.2596822458839));
#166828=CARTESIAN_POINT('Ctrl Pts',(-19.4967680143858,-16.9758594737003,
15.2640704548148));
#166829=CARTESIAN_POINT('Ctrl Pts',(-19.4284659821152,-16.9508253061037,
15.2684586637457));
#166830=CARTESIAN_POINT('Ctrl Pts',(-19.3589476876738,-16.9293459545263,
15.2728468726766));
#166831=CARTESIAN_POINT('Ctrl Pts',(-19.2895325699075,-16.9078984818679,
15.2772285687779));
#166832=CARTESIAN_POINT('Ctrl Pts',(-19.2189052304797,-16.8899954929979,
15.2816102648792));
#166833=CARTESIAN_POINT('Ctrl Pts',(-19.1474611885818,-16.8757681137367,
15.2859919609804));
#166834=CARTESIAN_POINT('Ctrl Pts',(-19.0761010991188,-16.8615574527783,
15.2903685082401));
#166835=CARTESIAN_POINT('Ctrl Pts',(-19.0039266843571,-16.8510139151847,
15.2947450554997));
#166836=CARTESIAN_POINT('Ctrl Pts',(-18.9313473123121,-16.84421845574,15.2991216027594));
#166837=CARTESIAN_POINT('Ctrl Pts',(-18.85881396905,-16.8374273058769,15.3034953744764));
#166838=CARTESIAN_POINT('Ctrl Pts',(-18.7858766571603,-16.8343795627893,
15.3078691461934));
#166839=CARTESIAN_POINT('Ctrl Pts',(-18.7129521899217,-16.8351046342129,
15.3122429179103));
#166840=CARTESIAN_POINT('Ctrl Pts',(-18.6400499138434,-16.8358294849948,
15.3166153586739));
#166841=CARTESIAN_POINT('Ctrl Pts',(-18.5671609567202,-16.840324866202,
15.3209877994375));
#166842=CARTESIAN_POINT('Ctrl Pts',(-18.4947027860634,-16.8485680796845,
15.325360240201));
#166843=CARTESIAN_POINT('Ctrl Pts',(-18.4222427626431,-16.8568115039469,
15.3297327927684));
#166844=CARTESIAN_POINT('Ctrl Pts',(-18.3502140266188,-16.8688028942382,
15.3341053453357));
#166845=CARTESIAN_POINT('Ctrl Pts',(-18.2790278943149,-16.8844678036247,
15.3384778979031));
#166846=CARTESIAN_POINT('Ctrl Pts',(-18.2077678823577,-16.9001489706451,
15.3428549884704));
#166847=CARTESIAN_POINT('Ctrl Pts',(-18.1373526922048,-16.9195111648158,
15.3472320790378));
#166848=CARTESIAN_POINT('Ctrl Pts',(-18.068181604065,-16.9424291842201,
15.3516091696051));
#166849=CARTESIAN_POINT('Ctrl Pts',(-17.9989727390266,-16.9653597200053,
15.355988650664));
#166850=CARTESIAN_POINT('Ctrl Pts',(-17.9310097785358,-16.9918497721616,
15.360368131723));
#166851=CARTESIAN_POINT('Ctrl Pts',(-17.8646724802095,-17.0217257543719,
15.3647476127819));
#166852=CARTESIAN_POINT('Ctrl Pts',(-17.7982175994673,-17.0516546915603,
15.3691348564417));
#166853=CARTESIAN_POINT('Ctrl Pts',(-17.7333945644586,-17.0849813228793,
15.3735221001014));
#166854=CARTESIAN_POINT('Ctrl Pts',(-17.67055844431,-17.1214861219779,15.3779093437611));
#166855=CARTESIAN_POINT('Ctrl Pts',(-17.627835937484,-17.1463058677703,
15.3808922466959));
#166856=CARTESIAN_POINT('Ctrl Pts',(-17.5860313573343,-17.1725938434286,
15.3838751496307));
#166857=CARTESIAN_POINT('Ctrl Pts',(-17.5452478505357,-17.2002701900282,
15.3868580525654));
#166858=CARTESIAN_POINT('Ctrl Pts',(-17.4852504075478,-17.2409854241403,
15.3912462614963));
#166859=CARTESIAN_POINT('Ctrl Pts',(-17.4272300397247,-17.2848661041391,
15.3956344704272));
#166860=CARTESIAN_POINT('Ctrl Pts',(-17.3715403699669,-17.3316936226349,
15.4000226793581));
#166861=CARTESIAN_POINT('Ctrl Pts',(-17.3159333529126,-17.378451641329,
15.4044043754593));
#166862=CARTESIAN_POINT('Ctrl Pts',(-17.2626505332037,-17.4281475084506,
15.4087860715606));
#166863=CARTESIAN_POINT('Ctrl Pts',(-17.2120162539407,-17.4805196308712,
15.4131677676619));
#166864=CARTESIAN_POINT('Ctrl Pts',(-17.1614414739856,-17.5328302118801,
15.4175443149215));
#166865=CARTESIAN_POINT('Ctrl Pts',(-17.1135093856061,-17.5878104559202,
15.4219208621811));
#166866=CARTESIAN_POINT('Ctrl Pts',(-17.0685096421066,-17.6451599685638,
15.4262974094408));
#166867=CARTESIAN_POINT('Ctrl Pts',(-17.0235384367905,-17.70247311098,15.4306711811577));
#166868=CARTESIAN_POINT('Ctrl Pts',(-16.9814961836094,-17.7621521621708,
15.4350449528747));
#166869=CARTESIAN_POINT('Ctrl Pts',(-16.9426332229373,-17.8238625659805,
15.4394187245917));
#166870=CARTESIAN_POINT('Ctrl Pts',(-16.9037820883947,-17.8855541911071,
15.4437911653552));
#166871=CARTESIAN_POINT('Ctrl Pts',(-16.8681085825381,-17.9492755337056,
15.4481636061187));
#166872=CARTESIAN_POINT('Ctrl Pts',(-16.8358195870614,-18.0146632835868,
15.4525360468823));
#166873=CARTESIAN_POINT('Ctrl Pts',(-16.8035297659516,-18.0800527054399,
15.4569085994496));
#166874=CARTESIAN_POINT('Ctrl Pts',(-16.774624838831,-18.1471081857714,
15.461281152017));
#166875=CARTESIAN_POINT('Ctrl Pts',(-16.7492648453349,-18.2154435759314,
15.4656537045843));
#166876=CARTESIAN_POINT('Ctrl Pts',(-16.7238785322811,-18.2838498871369,
15.4700307951516));
#166877=CARTESIAN_POINT('Ctrl Pts',(-16.7020446665449,-18.3535383070813,
15.4744078857189));
#166878=CARTESIAN_POINT('Ctrl Pts',(-16.6838740959319,-18.4241053348735,
15.4787849762862));
#166879=CARTESIAN_POINT('Ctrl Pts',(-16.665693601696,-18.4947109019386,
15.4831644573452));
#166880=CARTESIAN_POINT('Ctrl Pts',(-16.6511804819233,-18.566195559148,
15.4875439384041));
#166881=CARTESIAN_POINT('Ctrl Pts',(-16.6403943335878,-18.6381460314626,
15.491923419463));
#166882=CARTESIAN_POINT('Ctrl Pts',(-16.6295890668767,-18.7102240355065,
15.4963106631227));
#166883=CARTESIAN_POINT('Ctrl Pts',(-16.6225240103779,-18.7827690229242,
15.5006979067824));
#166884=CARTESIAN_POINT('Ctrl Pts',(-16.6192067693547,-18.855363611321,
15.5050851504422));
#166885=CARTESIAN_POINT('Ctrl Pts',(-16.6169513651075,-18.9047209362344,
15.5080680533771));
#166886=CARTESIAN_POINT('Ctrl Pts',(-16.6164273661252,-18.9541011550573,
15.511050956312));
#166887=CARTESIAN_POINT('Ctrl Pts',(-16.6176234550289,-19.0033743116383,
15.5140338592469));
#166888=CARTESIAN_POINT('Ctrl Pts',(-16.6193830456439,-19.0758610503895,
15.5184220681778));
#166889=CARTESIAN_POINT('Ctrl Pts',(-16.6248744285954,-19.1483987776271,
15.5228102771086));
#166890=CARTESIAN_POINT('Ctrl Pts',(-16.6341051990331,-19.2205718244199,
15.5271984860395));
#166891=CARTESIAN_POINT('Ctrl Pts',(-16.643322269477,-19.2926377544447,
15.5315801821408));
#166892=CARTESIAN_POINT('Ctrl Pts',(-16.6562676494649,-19.3643396039473,
15.5359618782421));
#166893=CARTESIAN_POINT('Ctrl Pts',(-16.6728969413427,-19.4352630563096,
15.5403435743433));
#166894=CARTESIAN_POINT('Ctrl Pts',(-16.6895066924792,-19.506103167971,
15.544720121603));
#166895=CARTESIAN_POINT('Ctrl Pts',(-16.7097916465688,-19.576166232197,
15.5490966688626));
#166896=CARTESIAN_POINT('Ctrl Pts',(-16.7336560032764,-19.6450460985908,
15.5534732161223));
#166897=CARTESIAN_POINT('Ctrl Pts',(-16.7575052255558,-19.7138822823745,
15.5578469878392));
#166898=CARTESIAN_POINT('Ctrl Pts',(-16.7849291889403,-19.7815363024759,
15.5622207595562));
#166899=CARTESIAN_POINT('Ctrl Pts',(-16.8157820891438,-19.8476165733563,
15.5665945312732));
#166900=CARTESIAN_POINT('Ctrl Pts',(-16.8466256007062,-19.9136767357882,
15.5709669720367));
#166901=CARTESIAN_POINT('Ctrl Pts',(-16.8808957735919,-19.9781636629368,
15.5753394128003));
#166902=CARTESIAN_POINT('Ctrl Pts',(-16.9183991025641,-20.0407067471224,
15.5797118535638));
#166903=CARTESIAN_POINT('Ctrl Pts',(-16.9559033905005,-20.1032514305415,
15.5840844061312));
#166904=CARTESIAN_POINT('Ctrl Pts',(-16.9966407488745,-20.1638517596418,
15.5884569586985));
#166905=CARTESIAN_POINT('Ctrl Pts',(-17.0403731142002,-20.2221641514765,
15.5928295112658));
#166906=CARTESIAN_POINT('Ctrl Pts',(-17.0841508666242,-20.280537062111,
15.5972066018332));
#166907=CARTESIAN_POINT('Ctrl Pts',(-17.1309295419551,-20.3366169078816,
15.6015836924005));
#166908=CARTESIAN_POINT('Ctrl Pts',(-17.1804298596136,-20.3900920759463,
15.6059607829678));
#166909=CARTESIAN_POINT('Ctrl Pts',(-17.2299572112327,-20.4435964487851,
15.6103402640268));
#166910=CARTESIAN_POINT('Ctrl Pts',(-17.2822088187839,-20.4944929748966,
15.6147197450857));
#166911=CARTESIAN_POINT('Ctrl Pts',(-17.3368694420731,-20.5425078447171,
15.6190992261446));
#166912=CARTESIAN_POINT('Ctrl Pts',(-17.3916269509501,-20.5906078205721,
15.6234864698044));
#166913=CARTESIAN_POINT('Ctrl Pts',(-17.4488016237921,-20.6358156407829,
15.6278737134641));
#166914=CARTESIAN_POINT('Ctrl Pts',(-17.5080466246419,-20.6778989893525,
15.6322609571238));
#166915=CARTESIAN_POINT('Ctrl Pts',(-17.5483275163853,-20.7065116112382,
15.6352438600586));
#166916=CARTESIAN_POINT('Ctrl Pts',(-17.5895648351146,-20.7336807873359,
15.6382267629935));
#166917=CARTESIAN_POINT('Ctrl Pts',(-17.6316431823902,-20.7593456909704,
15.6412096659283));
#166918=CARTESIAN_POINT('Ctrl Pts',(-17.6935454914315,-20.7971018505908,
15.6455978748592));
#166919=CARTESIAN_POINT('Ctrl Pts',(-17.7575106221337,-20.8317477625257,
15.6499860837901));
#166920=CARTESIAN_POINT('Ctrl Pts',(-17.8231931738168,-20.8630520467476,
15.654374292721));
#166921=CARTESIAN_POINT('Ctrl Pts',(-17.8887782417028,-20.8943098702212,
15.6587559888223));
#166922=CARTESIAN_POINT('Ctrl Pts',(-17.9560752387298,-20.9222357055048,
15.6631376849236));
#166923=CARTESIAN_POINT('Ctrl Pts',(-18.0247117585808,-20.9466426222721,
15.6675193810248));
#166924=CARTESIAN_POINT('Ctrl Pts',(-18.0932676250588,-20.9710208589698,
15.6718959282845));
#166925=CARTESIAN_POINT('Ctrl Pts',(-18.1631594352668,-20.9918882305584,
15.6762724755441));
#166926=CARTESIAN_POINT('Ctrl Pts',(-18.2339938260915,-21.0091054484526,
15.6806490228038));
#166927=CARTESIAN_POINT('Ctrl Pts',(-18.304783294775,-21.0263117474375,
15.6850227945208));
#166928=CARTESIAN_POINT('Ctrl Pts',(-18.376513690443,-21.0398723720884,
15.6893965662377));
#166929=CARTESIAN_POINT('Ctrl Pts',(-18.4487768305325,-21.0496979629105,
15.6937703379547));
#166930=CARTESIAN_POINT('Ctrl Pts',(-18.5210179807058,-21.0595205637724,
15.6981427787183));
#166931=CARTESIAN_POINT('Ctrl Pts',(-18.5937910757581,-21.0656103223221,
15.7025152194818));
#166932=CARTESIAN_POINT('Ctrl Pts',(-18.6666797525664,-21.0679293429331,
15.7068876602454));
#166933=CARTESIAN_POINT('Ctrl Pts',(-18.7395702931462,-21.0702484228418,
15.7112602128128));
#166934=CARTESIAN_POINT('Ctrl Pts',(-18.8125759391524,-21.0687965600418,
15.7156327653801));
#166935=CARTESIAN_POINT('Ctrl Pts',(-18.8852789324503,-21.0635879533178,
15.7200053179475));
#166936=CARTESIAN_POINT('Ctrl Pts',(-18.958057379657,-21.0583739409052,
15.7243824085148));
#166937=CARTESIAN_POINT('Ctrl Pts',(-19.030532064851,-21.0493954347149,
15.7287594990821));
#166938=CARTESIAN_POINT('Ctrl Pts',(-19.1022898016655,-21.0367185953958,
15.7331365896495));
#166939=CARTESIAN_POINT('Ctrl Pts',(-19.1740867280434,-21.0240348327843,
15.7375160707084));
#166940=CARTESIAN_POINT('Ctrl Pts',(-19.2451654560907,-21.007648824085,
15.7418955517674));
#166941=CARTESIAN_POINT('Ctrl Pts',(-19.3151251217576,-20.9876774284896,
15.7462750328263));
#166942=CARTESIAN_POINT('Ctrl Pts',(-19.3852087904624,-20.9676706337297,
15.750662276486));
#166943=CARTESIAN_POINT('Ctrl Pts',(-19.4541689789729,-20.9440659176035,
15.7550495201458));
#166944=CARTESIAN_POINT('Ctrl Pts',(-19.5216226105755,-20.9170291660203,
15.7594367638055));
#166945=CARTESIAN_POINT('Ctrl Pts',(-19.5674845802478,-20.8986467801992,
15.7624196667403));
#166946=CARTESIAN_POINT('Ctrl Pts',(-19.6126505362301,-20.8786788808129,
15.765402569675));
#166947=CARTESIAN_POINT('Ctrl Pts',(-19.6570068699279,-20.8571895753615,
15.7683854726098));
#166948=CARTESIAN_POINT('Ctrl Pts',(-19.7222603709407,-20.8255762228108,
15.7727736815407));
#166949=CARTESIAN_POINT('Ctrl Pts',(-19.7860152120979,-20.7905448456105,
15.7771618904716));
#166950=CARTESIAN_POINT('Ctrl Pts',(-19.8478898805759,-20.7522606294508,
15.7815500994025));
#166951=CARTESIAN_POINT('Ctrl Pts',(-19.9096727167869,-20.7140332334156,
15.7859317955037));
#166952=CARTESIAN_POINT('Ctrl Pts',(-19.9695805130032,-20.6725628338803,
15.790313491605));
#166953=CARTESIAN_POINT('Ctrl Pts',(-20.027254513927,-20.6280613837827,
15.7946951877063));
#166954=CARTESIAN_POINT('Ctrl Pts',(-20.0848607433098,-20.5836122264305,
15.7990717349659));
#166955=CARTESIAN_POINT('Ctrl Pts',(-20.1402380117451,-20.5361393871243,
15.8034482822255));
#166956=CARTESIAN_POINT('Ctrl Pts',(-20.1930562795832,-20.485898227722,
15.8078248294852));
#166957=CARTESIAN_POINT('Ctrl Pts',(-20.2458410508435,-20.4356889305328,
15.8121986012022));
#166958=CARTESIAN_POINT('Ctrl Pts',(-20.2960696928601,-20.3827151282833,
15.8165723729191));
#166959=CARTESIAN_POINT('Ctrl Pts',(-20.3434461269596,-20.3272716693129,
15.8209461446361));
#166960=CARTESIAN_POINT('Ctrl Pts',(-20.3908081442512,-20.2718450819733,
15.8253185853997));
#166961=CARTESIAN_POINT('Ctrl Pts',(-20.4353193635672,-20.2139506964278,
15.8296910261632));
#166962=CARTESIAN_POINT('Ctrl Pts',(-20.4767225512214,-20.1539180959884,
15.8340634669268));
#166963=CARTESIAN_POINT('Ctrl Pts',(-20.5181267975597,-20.0938839605087,
15.8384360194941));
#166964=CARTESIAN_POINT('Ctrl Pts',(-20.5564225822287,-20.0317118998147,
15.8428085720614));
#166965=CARTESIAN_POINT('Ctrl Pts',(-20.5913957196045,-19.9677608679186,
15.8471811246288));
#166966=CARTESIAN_POINT('Ctrl Pts',(-20.6264051534215,-19.9037434652295,
15.8515582151961));
#166967=CARTESIAN_POINT('Ctrl Pts',(-20.6580848230993,-19.8379438292391,
15.8559353057634));
#166968=CARTESIAN_POINT('Ctrl Pts',(-20.6862667093298,-19.7707451957981,
15.8603123963308));
#166969=CARTESIAN_POINT('Ctrl Pts',(-20.7144639867344,-19.7035098626893,
15.8646918773897));
#166970=CARTESIAN_POINT('Ctrl Pts',(-20.7391595139378,-19.6348744651304,
15.8690713584487));
#166971=CARTESIAN_POINT('Ctrl Pts',(-20.7602345709195,-19.5652393200134,
15.8734508395076));
#166972=CARTESIAN_POINT('Ctrl Pts',(-20.7813469832984,-19.4954807470691,
15.8778380831673));
#166973=CARTESIAN_POINT('Ctrl Pts',(-20.798825994671,-19.424719356578,15.882225326827));
#166974=CARTESIAN_POINT('Ctrl Pts',(-20.8126037366754,-19.3533670463295,
15.8866125704868));
#166975=CARTESIAN_POINT('Ctrl Pts',(-20.8219712736182,-19.3048543508528,
15.8895954734216));
#166976=CARTESIAN_POINT('Ctrl Pts',(-20.8296289055562,-19.2560686843217,
15.8925783763564));
#166977=CARTESIAN_POINT('Ctrl Pts',(-20.8355690425742,-19.207140273759,
15.8955612792912));
#166978=CARTESIAN_POINT('Ctrl Pts',(-20.8457798800575,-19.1230344615427,
15.9006887598533));
#166979=CARTESIAN_POINT('Ctrl Pts',(-20.850943223371,-19.0383036553196,
15.9058162404154));
#166980=CARTESIAN_POINT('Ctrl Pts',(-20.8509995343428,-18.9534041339616,
15.9109437209775));
#166981=CARTESIAN_POINT('',(-20.8509995791063,-18.9533349395905,15.6876313735509));
#166982=CARTESIAN_POINT('Ctrl Pts',(-20.7225805503655,-18.2258895437275,
14.9318514930297));
#166983=CARTESIAN_POINT('Ctrl Pts',(-20.7140100821148,-18.2024178166321,
14.9332895026011));
#166984=CARTESIAN_POINT('Ctrl Pts',(-20.7050225797307,-18.179093798098,
14.9347403257965));
#166985=CARTESIAN_POINT('Ctrl Pts',(-20.6902873303515,-18.1427842636067,
14.9370362637722));
#166986=CARTESIAN_POINT('Ctrl Pts',(-20.6848211899767,-18.1296941584371,
14.9378717048454));
#166987=CARTESIAN_POINT('Ctrl Pts',(-20.6758998533147,-18.1089193810253,
14.9392103882356));
#166988=CARTESIAN_POINT('Ctrl Pts',(-20.6725295621615,-18.1011985520166,
14.9397107437133));
#166989=CARTESIAN_POINT('Ctrl Pts',(-20.6664968922938,-18.0876005621048,
14.9405970906885));
#166990=CARTESIAN_POINT('Ctrl Pts',(-20.6638535463659,-18.0817150379815,
14.9409824261025));
#166991=CARTESIAN_POINT('Ctrl Pts',(-20.6583232649041,-18.069550721461,
14.9417824220348));
#166992=CARTESIAN_POINT('Ctrl Pts',(-20.6554324098596,-18.0632738050306,
14.9421972141488));
#166993=CARTESIAN_POINT('Ctrl Pts',(-20.6479172888172,-18.0471642829473,
14.9432669413107));
#166994=CARTESIAN_POINT('Ctrl Pts',(-20.6432480047396,-18.0373530119265,
14.9439234292868));
#166995=CARTESIAN_POINT('Ctrl Pts',(-20.623305154258,-17.9962665399389,
14.9466939274273));
#166996=CARTESIAN_POINT('Ctrl Pts',(-20.60733773314,-17.9653359617657,14.9488320096977));
#166997=CARTESIAN_POINT('Ctrl Pts',(-20.563605069465,-17.8855130100752,
14.9544918546439));
#166998=CARTESIAN_POINT('Ctrl Pts',(-20.5346433137451,-17.8373108063542,
14.9580538430729));
#166999=CARTESIAN_POINT('Ctrl Pts',(-20.4347647586242,-17.6851473573637,
14.969763671701));
#167000=CARTESIAN_POINT('Ctrl Pts',(-20.3564957391982,-17.5863429069977,
14.9781231163307));
#167001=CARTESIAN_POINT('Ctrl Pts',(-20.2011023779936,-17.4225225399811,
14.9930006084852));
#167002=CARTESIAN_POINT('Ctrl Pts',(-20.1272128098503,-17.3549234499617,
14.9995201870726));
#167003=CARTESIAN_POINT('Ctrl Pts',(-20.0412146212309,-17.2867754181238,
15.0062995681532));
#167004=CARTESIAN_POINT('Ctrl Pts',(-20.0335754769467,-17.2808068448063,
15.0068951999125));
#167005=CARTESIAN_POINT('Ctrl Pts',(-20.0222359690359,-17.2720718985144,
15.0077693581891));
#167006=CARTESIAN_POINT('Ctrl Pts',(-20.018567242737,-17.2692649234357,
15.0080506501258));
#167007=CARTESIAN_POINT('Ctrl Pts',(-20.0120424365972,-17.2643065102165,
15.0085481761867));
#167008=CARTESIAN_POINT('Ctrl Pts',(-20.0091900671863,-17.2621502793356,
15.0087647451505));
#167009=CARTESIAN_POINT('Ctrl Pts',(-20.0030671640945,-17.2575460403536,
15.0092276374586));
#167010=CARTESIAN_POINT('Ctrl Pts',(-19.9997950128624,-17.2551002756775,
15.0094738045857));
#167011=CARTESIAN_POINT('Ctrl Pts',(-19.9907938693459,-17.2484129075098,
15.0101477229807));
#167012=CARTESIAN_POINT('Ctrl Pts',(-19.9850504408161,-17.2441906987168,
15.0105741421245));
#167013=CARTESIAN_POINT('Ctrl Pts',(-19.9542778887906,-17.2218071920604,
15.0128403741077));
#167014=CARTESIAN_POINT('Ctrl Pts',(-19.9288730082408,-17.2041659118355,
15.0146464521655));
#167015=CARTESIAN_POINT('Ctrl Pts',(-19.8508165898018,-17.1524608712662,
15.020031926796));
#167016=CARTESIAN_POINT('Ctrl Pts',(-19.7970274433944,-17.1201719036548,
15.023524573912));
#167017=CARTESIAN_POINT('Ctrl Pts',(-19.6236648901271,-17.0263166627344,
15.0343589449834));
#167018=CARTESIAN_POINT('Ctrl Pts',(-19.4996237033979,-16.9737227247783,
15.0415276930897));
#167019=CARTESIAN_POINT('Ctrl Pts',(-19.3325235182404,-16.9209600284138,
15.0512527370378));
#167020=CARTESIAN_POINT('Ctrl Pts',(-19.2932700150733,-16.9098025137702,
15.0535399696008));
#167021=CARTESIAN_POINT('Ctrl Pts',(-19.2066105138334,-16.8878561237639,
15.0586207112253));
#167022=CARTESIAN_POINT('Ctrl Pts',(-19.1591071714363,-16.8775521217728,
15.0614260183341));
#167023=CARTESIAN_POINT('Ctrl Pts',(-19.0988926664441,-16.8666460307821,
15.0650250366351));
#167024=CARTESIAN_POINT('Ctrl Pts',(-19.086471857336,-16.8645107390911,
15.0657696811737));
#167025=CARTESIAN_POINT('Ctrl Pts',(-19.0667599296158,-16.861302956798,
15.066955287616));
#167026=CARTESIAN_POINT('Ctrl Pts',(-19.059480879897,-16.8601573931273,
15.0673939267733));
#167027=CARTESIAN_POINT('Ctrl Pts',(-19.0459068961037,-16.8580937088595,
15.0682135031394));
#167028=CARTESIAN_POINT('Ctrl Pts',(-19.0396135007279,-16.8571659123645,
15.0685941287033));
#167029=CARTESIAN_POINT('Ctrl Pts',(-19.0256263806054,-16.8551682490841,
15.0694415329751));
#167030=CARTESIAN_POINT('Ctrl Pts',(-19.0179307843542,-16.8541123374447,
15.0699087479767));
#167031=CARTESIAN_POINT('Ctrl Pts',(-18.9955533550318,-16.8511673159892,
15.0712702582554));
#167032=CARTESIAN_POINT('Ctrl Pts',(-18.9808575273109,-16.84938984415,15.0721680618509));
#167033=CARTESIAN_POINT('Ctrl Pts',(-18.8639365135023,-16.8364908104568,
15.0793414308601));
#167034=CARTESIAN_POINT('Ctrl Pts',(-18.7610580396062,-16.8326781614781,
15.0858478166534));
#167035=CARTESIAN_POINT('Ctrl Pts',(-18.5026305788978,-16.8419222680883,
15.1026339664158));
#167036=CARTESIAN_POINT('Ctrl Pts',(-18.3480409092547,-16.8646591784076,
15.1131042240962));
#167037=CARTESIAN_POINT('Ctrl Pts',(-18.1465341195476,-16.9174650569955,
15.1265601184731));
#167038=CARTESIAN_POINT('Ctrl Pts',(-18.0962266236068,-16.9326697371415,
15.1298979314946));
#167039=CARTESIAN_POINT('Ctrl Pts',(-18.0383148603353,-16.9525534059556,
15.1336748472197));
#167040=CARTESIAN_POINT('Ctrl Pts',(-18.0301141996943,-16.9554256131912,
15.134208118171));
#167041=CARTESIAN_POINT('Ctrl Pts',(-18.0177156732353,-16.9598539707664,
15.1350117425559));
#167042=CARTESIAN_POINT('Ctrl Pts',(-18.0135047923686,-16.9613730396702,
15.1352842147549));
#167043=CARTESIAN_POINT('Ctrl Pts',(-18.0059505398211,-16.964125335466,
15.1357721560182));
#167044=CARTESIAN_POINT('Ctrl Pts',(-18.0026054509707,-16.9653536518565,
15.1359879109025));
#167045=CARTESIAN_POINT('Ctrl Pts',(-17.9953385778605,-16.9680428892514,
15.1364559388706));
#167046=CARTESIAN_POINT('Ctrl Pts',(-17.9914180318467,-16.9695069898947,
15.1367080190812));
#167047=CARTESIAN_POINT('Ctrl Pts',(-17.980404769588,-16.9736570699484,
15.1374150125109));
#167048=CARTESIAN_POINT('Ctrl Pts',(-17.9733220257991,-16.9763695832229,
15.1378683677725));
#167049=CARTESIAN_POINT('Ctrl Pts',(-17.9308016113123,-16.992916400669,
15.1405829504437));
#167050=CARTESIAN_POINT('Ctrl Pts',(-17.8957251244416,-17.0076667364892,
15.1427926455673));
#167051=CARTESIAN_POINT('Ctrl Pts',(-17.7810024653374,-17.059592150679,
15.1499807157809));
#167052=CARTESIAN_POINT('Ctrl Pts',(-17.7032694218125,-17.1007818357106,
15.1547897428524));
#167053=CARTESIAN_POINT('Ctrl Pts',(-17.4797369312111,-17.2376867240354,
15.1690494204472));
#167054=CARTESIAN_POINT('Ctrl Pts',(-17.3429765256505,-17.3466673888159,
15.1784224143218));
#167055=CARTESIAN_POINT('Ctrl Pts',(-17.204968133178,-17.4876628048802,
15.1898859848335));
#167056=CARTESIAN_POINT('Ctrl Pts',(-17.1890923572652,-17.5044219590816,
15.1912382901944));
#167057=CARTESIAN_POINT('Ctrl Pts',(-17.1670331084522,-17.5284849204347,
15.1931673993233));
#167058=CARTESIAN_POINT('Ctrl Pts',(-17.160619875148,-17.5355765466786,
15.1937344267605));
#167059=CARTESIAN_POINT('Ctrl Pts',(-17.1502809956308,-17.5471659344809,
15.1946587768455));
#167060=CARTESIAN_POINT('Ctrl Pts',(-17.1463259017311,-17.5516373351859,
15.1950148579219));
#167061=CARTESIAN_POINT('Ctrl Pts',(-17.1380892620196,-17.5610289520697,
15.1957616480098));
#167062=CARTESIAN_POINT('Ctrl Pts',(-17.1338114421202,-17.5659523393713,
15.1961525064804));
#167063=CARTESIAN_POINT('Ctrl Pts',(-17.1236935747793,-17.5777063704543,
15.1970841833849));
#167064=CARTESIAN_POINT('Ctrl Pts',(-17.1178741720236,-17.5845545467654,
15.1976258447062));
#167065=CARTESIAN_POINT('Ctrl Pts',(-17.0984378080704,-17.6077243104415,
15.1994547520618));
#167066=CARTESIAN_POINT('Ctrl Pts',(-17.0850234453315,-17.6242134645767,
15.200750187143));
#167067=CARTESIAN_POINT('Ctrl Pts',(-17.0134816870639,-17.7149102380274,
15.207844884841));
#167068=CARTESIAN_POINT('Ctrl Pts',(-16.9601191872357,-17.7927256160896,
15.213829198846));
#167069=CARTESIAN_POINT('Ctrl Pts',(-16.8276093320395,-18.016638557212,
15.2307280904052));
#167070=CARTESIAN_POINT('Ctrl Pts',(-16.7601847899077,-18.1688803243164,
15.2419108154703));
#167071=CARTESIAN_POINT('Ctrl Pts',(-16.6988392690935,-18.3675569577416,
15.2552397293083));
#167072=CARTESIAN_POINT('Ctrl Pts',(-16.687644510726,-18.4080490597497,
15.2578906944697));
#167073=CARTESIAN_POINT('Ctrl Pts',(-16.675893492263,-18.4560746848134,
15.2609373419138));
#167074=CARTESIAN_POINT('Ctrl Pts',(-16.6741638822505,-18.4633083925592,
15.2613936515972));
#167075=CARTESIAN_POINT('Ctrl Pts',(-16.6714258402955,-18.4750324822145,
15.2621288768928));
#167076=CARTESIAN_POINT('Ctrl Pts',(-16.6703938825172,-18.4795172277065,
15.2624090925418));
#167077=CARTESIAN_POINT('Ctrl Pts',(-16.6685864919216,-18.4874907825841,
15.2629054309221));
#167078=CARTESIAN_POINT('Ctrl Pts',(-16.6678052627434,-18.4909782208841,
15.2631218825314));
#167079=CARTESIAN_POINT('Ctrl Pts',(-16.666147560555,-18.498467125969,15.2635853189283));
#167080=CARTESIAN_POINT('Ctrl Pts',(-16.6652738711421,-18.5024691516922,
15.2638321433353));
#167081=CARTESIAN_POINT('Ctrl Pts',(-16.6629010519147,-18.513491529012,
15.2645097179222));
#167082=CARTESIAN_POINT('Ctrl Pts',(-16.6614259895895,-18.5205170842103,
15.2649391117915));
#167083=CARTESIAN_POINT('Ctrl Pts',(-16.6536452675477,-18.5585364641904,
15.2672500552113));
#167084=CARTESIAN_POINT('Ctrl Pts',(-16.6479986932256,-18.5896629236122,
15.269096273308));
#167085=CARTESIAN_POINT('Ctrl Pts',(-16.6174873072952,-18.7823506489699,
15.2803088500755));
#167086=CARTESIAN_POINT('Ctrl Pts',(-16.6107040317,-18.9462297264881,15.2889470397337));
#167087=CARTESIAN_POINT('Ctrl Pts',(-16.6315477623825,-19.2260281016585,
15.3043057725485));
#167088=CARTESIAN_POINT('Ctrl Pts',(-16.6499147915423,-19.3418465995857,
15.31084104163));
#167089=CARTESIAN_POINT('Ctrl Pts',(-16.6811576404712,-19.4694278135802,
15.3185359899385));
#167090=CARTESIAN_POINT('Ctrl Pts',(-16.6846978343963,-19.4832757424116,
15.3193776890723));
#167091=CARTESIAN_POINT('Ctrl Pts',(-16.6905550894349,-19.5052570792134,
15.320724517713));
#167092=CARTESIAN_POINT('Ctrl Pts',(-16.6927811664494,-19.5134144356961,
15.3212267042999));
#167093=CARTESIAN_POINT('Ctrl Pts',(-16.6967932181768,-19.5277770582127,
15.3221151819242));
#167094=CARTESIAN_POINT('Ctrl Pts',(-16.6985588351089,-19.5339879341633,
15.3225008066207));
#167095=CARTESIAN_POINT('Ctrl Pts',(-16.7022693173298,-19.5468167891505,
15.3233003087764));
#167096=CARTESIAN_POINT('Ctrl Pts',(-16.704218166859,-19.5534335272145,
15.3237143124345));
#167097=CARTESIAN_POINT('Ctrl Pts',(-16.7093033188198,-19.5703923870958,
15.3247796964519));
#167098=CARTESIAN_POINT('Ctrl Pts',(-16.7124865131509,-19.5807201371872,
15.3254326056138));
#167099=CARTESIAN_POINT('Ctrl Pts',(-16.7260999466082,-19.6237159837186,
15.3281682126281));
#167100=CARTESIAN_POINT('Ctrl Pts',(-16.7372436280267,-19.6561510932417,
15.3302742321447));
#167101=CARTESIAN_POINT('Ctrl Pts',(-16.7683257596659,-19.7399386426837,
15.3358290190082));
#167102=CARTESIAN_POINT('Ctrl Pts',(-16.7894883421232,-19.7908063640503,
15.3393161771292));
#167103=CARTESIAN_POINT('Ctrl Pts',(-16.8585268381152,-19.9400545332637,
15.3498858524371));
#167104=CARTESIAN_POINT('Ctrl Pts',(-16.9120657081409,-20.0356066220399,
15.3571167600105));
#167105=CARTESIAN_POINT('Ctrl Pts',(-16.9983226644594,-20.1649464433047,
15.3673863357202));
#167106=CARTESIAN_POINT('Ctrl Pts',(-17.0251516246502,-20.2024608410114,
15.3704263820036));
#167107=CARTESIAN_POINT('Ctrl Pts',(-17.0664519509549,-20.2563959180539,
15.3748627775964));
#167108=CARTESIAN_POINT('Ctrl Pts',(-17.0799865766435,-20.2735161172016,
15.3762811610953));
#167109=CARTESIAN_POINT('Ctrl Pts',(-17.1264767746259,-20.3304890602427,
15.3810284957954));
#167110=CARTESIAN_POINT('Ctrl Pts',(-17.1606297870683,-20.3693461598136,
15.3843124864419));
#167111=CARTESIAN_POINT('Ctrl Pts',(-17.2021187940727,-20.4131994318693,
15.388036017511));
#167112=CARTESIAN_POINT('Ctrl Pts',(-17.2081015600556,-20.4194460009142,
15.3885668262704));
#167113=CARTESIAN_POINT('Ctrl Pts',(-17.2172326797203,-20.428863520488,
15.3893674830195));
#167114=CARTESIAN_POINT('Ctrl Pts',(-17.2203529815626,-20.4320613725245,
15.3896394268918));
#167115=CARTESIAN_POINT('Ctrl Pts',(-17.2259797502575,-20.4377915805903,
15.3901268058044));
#167116=CARTESIAN_POINT('Ctrl Pts',(-17.2284824944755,-20.4403274961236,
15.3903425237122));
#167117=CARTESIAN_POINT('Ctrl Pts',(-17.2339435712008,-20.4458330831323,
15.3908109132161));
#167118=CARTESIAN_POINT('Ctrl Pts',(-17.2369043153148,-20.4488002810791,
15.3910633895394));
#167119=CARTESIAN_POINT('Ctrl Pts',(-17.2452686446277,-20.4571331968504,
15.3917726151543));
#167120=CARTESIAN_POINT('Ctrl Pts',(-17.2506924595149,-20.4624786436958,
15.3922277906716));
#167121=CARTESIAN_POINT('Ctrl Pts',(-17.2837764024432,-20.4947345053903,
15.3949766597113));
#167122=CARTESIAN_POINT('Ctrl Pts',(-17.3121411588994,-20.520915579421,
15.3972172955542));
#167123=CARTESIAN_POINT('Ctrl Pts',(-17.409050835543,-20.6055761451323,
15.4045584980955));
#167124=CARTESIAN_POINT('Ctrl Pts',(-17.4806134175529,-20.6604580795296,
15.4094813850064));
#167125=CARTESIAN_POINT('Ctrl Pts',(-17.6976245072979,-20.8058884037477,
15.4236863702818));
#167126=CARTESIAN_POINT('Ctrl Pts',(-17.8507979070175,-20.8835598809046,
15.4329073799991));
#167127=CARTESIAN_POINT('Ctrl Pts',(-18.0335321837806,-20.9498929075246,
15.4442004469876));
#167128=CARTESIAN_POINT('Ctrl Pts',(-18.0555494686134,-20.9574765131314,
15.4455643951208));
#167129=CARTESIAN_POINT('Ctrl Pts',(-18.0868087785433,-20.9676697602659,
15.4475072914679));
#167130=CARTESIAN_POINT('Ctrl Pts',(-18.0959508118928,-20.9705822471554,
15.448076270261));
#167131=CARTESIAN_POINT('Ctrl Pts',(-18.1108181498144,-20.9752076241768,
15.4490029353864));
#167132=CARTESIAN_POINT('Ctrl Pts',(-18.1165315292812,-20.9769586157422,
15.4493593675996));
#167133=CARTESIAN_POINT('Ctrl Pts',(-18.1284912799885,-20.9805686241052,
15.4501061920079));
#167134=CARTESIAN_POINT('Ctrl Pts',(-18.1347389670044,-20.9824230311866,
15.4504967305619));
#167135=CARTESIAN_POINT('Ctrl Pts',(-18.149594736269,-20.9867579067292,
15.4514263548101));
#167136=CARTESIAN_POINT('Ctrl Pts',(-18.158210144992,-20.9892126276577,
15.4519662735384));
#167137=CARTESIAN_POINT('Ctrl Pts',(-18.1871580384758,-20.9972622274732,
15.4537832151529));
#167138=CARTESIAN_POINT('Ctrl Pts',(-18.2075579831668,-21.0026078275547,
15.4550682818953));
#167139=CARTESIAN_POINT('Ctrl Pts',(-18.3182122525613,-21.0298436811777,
15.4620659767638));
#167140=CARTESIAN_POINT('Ctrl Pts',(-18.4097416493751,-21.04607888967,15.4679580387461));
#167141=CARTESIAN_POINT('Ctrl Pts',(-18.6541252393588,-21.0730192659131,
15.4839156481026));
#167142=CARTESIAN_POINT('Ctrl Pts',(-18.8075774858957,-21.0732461727291,
15.4941917929603));
#167143=CARTESIAN_POINT('Ctrl Pts',(-18.9633199080035,-21.0565461675966,
15.5043285933707));
#167144=CARTESIAN_POINT('Ctrl Pts',(-18.9669302640211,-21.056149634434,
15.5045633939949));
#167145=CARTESIAN_POINT('Ctrl Pts',(-19.0222532155453,-21.0499292626121,
15.508158318721));
#167146=CARTESIAN_POINT('Ctrl Pts',(-19.0737396946946,-21.0422093238847,
15.5114638371581));
#167147=CARTESIAN_POINT('Ctrl Pts',(-19.1334072596646,-21.0309992503506,
15.5152085724859));
#167148=CARTESIAN_POINT('Ctrl Pts',(-19.141911257241,-21.0293474562839,
15.5157402182174));
#167149=CARTESIAN_POINT('Ctrl Pts',(-19.154788500525,-21.0267640892072,
15.5165418838924));
#167150=CARTESIAN_POINT('Ctrl Pts',(-19.1591692098003,-21.0258708088799,
15.5168140074847));
#167151=CARTESIAN_POINT('Ctrl Pts',(-19.1670361088122,-21.0242406772178,
15.5173015775243));
#167152=CARTESIAN_POINT('Ctrl Pts',(-19.170523280348,-21.0235088998456,
15.5175173078435));
#167153=CARTESIAN_POINT('Ctrl Pts',(-19.1781065376194,-21.0218975660512,
15.5179855736042));
#167154=CARTESIAN_POINT('Ctrl Pts',(-19.18220185192,-21.0210146571097,15.5182379145921));
#167155=CARTESIAN_POINT('Ctrl Pts',(-19.1937234716516,-21.0184948966738,
15.5189463773023));
#167156=CARTESIAN_POINT('Ctrl Pts',(-19.2011437039711,-21.0168301606141,
15.5194009306643));
#167157=CARTESIAN_POINT('Ctrl Pts',(-19.2459797007189,-21.006517097298,
15.522138015781));
#167158=CARTESIAN_POINT('Ctrl Pts',(-19.2831659926924,-20.9968914020362,
15.5243680167707));
#167159=CARTESIAN_POINT('Ctrl Pts',(-19.4059031199549,-20.961530689677,
15.5316563038228));
#167160=CARTESIAN_POINT('Ctrl Pts',(-19.4900899996355,-20.9313933011439,
15.5365398122478));
#167161=CARTESIAN_POINT('Ctrl Pts',(-19.730183897947,-20.8278817239532,
15.5507589194619));
#167162=CARTESIAN_POINT('Ctrl Pts',(-19.8793220881741,-20.7407272276739,
15.5600279547936));
#167163=CARTESIAN_POINT('Ctrl Pts',(-20.0347835024601,-20.6223871118364,
15.5713778662168));
#167164=CARTESIAN_POINT('Ctrl Pts',(-20.0530706137417,-20.6079841413669,
15.5727413092634));
#167165=CARTESIAN_POINT('Ctrl Pts',(-20.078553579852,-20.5872237469678,
15.5746836071848));
#167166=CARTESIAN_POINT('Ctrl Pts',(-20.0859497883209,-20.5811141141724,
15.5752525010511));
#167167=CARTESIAN_POINT('Ctrl Pts',(-20.0978850644286,-20.5711177340743,
15.5761790653872));
#167168=CARTESIAN_POINT('Ctrl Pts',(-20.1024497033832,-20.5672616239942,
15.5765354822846));
#167169=CARTESIAN_POINT('Ctrl Pts',(-20.1116089907752,-20.559457360816,
15.5772548405965));
#167170=CARTESIAN_POINT('Ctrl Pts',(-20.1162031386547,-20.5555087092422,
15.5776178006941));
#167171=CARTESIAN_POINT('Ctrl Pts',(-20.1271967570972,-20.545977388516,
15.5784915500211));
#167172=CARTESIAN_POINT('Ctrl Pts',(-20.1335796693684,-20.5403758575646,
15.5790031209341));
#167173=CARTESIAN_POINT('Ctrl Pts',(-20.153834463005,-20.5223837275505,
15.5806402947629));
#167174=CARTESIAN_POINT('Ctrl Pts',(-20.1675765342527,-20.509848914329,
15.5817719442139));
#167175=CARTESIAN_POINT('Ctrl Pts',(-20.1993790457063,-20.4800631366377,
15.5844410650096));
#167176=CARTESIAN_POINT('Ctrl Pts',(-20.21730261354,-20.4626707023589,15.5859844865919));
#167177=CARTESIAN_POINT('Ctrl Pts',(-20.2792768851416,-20.4003665062822,
15.5914623361029));
#167178=CARTESIAN_POINT('Ctrl Pts',(-20.3216264213745,-20.3538157325635,
15.595465872288));
#167179=CARTESIAN_POINT('Ctrl Pts',(-20.4170842132422,-20.2390057522114,
15.605120123752));
#167180=CARTESIAN_POINT('Ctrl Pts',(-20.4682073322372,-20.1692426219444,
15.6108203699025));
#167181=CARTESIAN_POINT('Ctrl Pts',(-20.5798191126562,-19.9955753179193,
15.6244629060589));
#167182=CARTESIAN_POINT('Ctrl Pts',(-20.6360168547679,-19.8892486639399,
15.6323956032691));
#167183=CARTESIAN_POINT('Ctrl Pts',(-20.6891096196537,-19.7640887067501,
15.6408791931028));
#167184=CARTESIAN_POINT('Ctrl Pts',(-20.6951525735272,-19.749384669021,
15.6418629227137));
#167185=CARTESIAN_POINT('Ctrl Pts',(-20.7031816721666,-19.7292042417736,
15.643194069304));
#167186=CARTESIAN_POINT('Ctrl Pts',(-20.7053115240518,-19.7237860897997,
15.6435496095536));
#167187=CARTESIAN_POINT('Ctrl Pts',(-20.7086560753642,-19.7151736771791,
15.6441117420015));
#167188=CARTESIAN_POINT('Ctrl Pts',(-20.7098854190927,-19.7119851896667,
15.6443192009855));
#167189=CARTESIAN_POINT('Ctrl Pts',(-20.7124047678474,-19.7054034460699,
15.6447460743496));
#167190=CARTESIAN_POINT('Ctrl Pts',(-20.713693765801,-19.7020098477928,
15.6449654224589));
#167191=CARTESIAN_POINT('Ctrl Pts',(-20.716738503589,-19.693931302329,15.645485833969));
#167192=CARTESIAN_POINT('Ctrl Pts',(-20.7184863900503,-19.6892433789904,
15.6457864284112));
#167193=CARTESIAN_POINT('Ctrl Pts',(-20.7242988977446,-19.6734834755288,
15.6467924261389));
#167194=CARTESIAN_POINT('Ctrl Pts',(-20.728287691953,-19.6623835047555,
15.6474934572906));
#167195=CARTESIAN_POINT('Ctrl Pts',(-20.7681644656086,-19.5484313285155,
15.6546191733456));
#167196=CARTESIAN_POINT('Ctrl Pts',(-20.7961606459488,-19.4429737431072,
15.6606275804652));
#167197=CARTESIAN_POINT('Ctrl Pts',(-20.8391772197475,-19.2096417403651,
15.6735634057899));
#167198=CARTESIAN_POINT('Ctrl Pts',(-20.8509186831227,-19.0816229643116,
15.6804481091254));
#167199=CARTESIAN_POINT('Ctrl Pts',(-20.8509995791063,-18.9533349395905,
15.6876313735509));
#167200=CARTESIAN_POINT('Ctrl Pts',(-20.8509995807916,-18.9533322642405,
15.6876315233525));
#167201=CARTESIAN_POINT('Ctrl Pts',(-20.8510434832008,-18.8835702913221,
15.6915377254668));
#167202=CARTESIAN_POINT('Ctrl Pts',(-20.8476390986516,-18.813853334251,
15.6955212716884));
#167203=CARTESIAN_POINT('Ctrl Pts',(-20.8397874096428,-18.7341582859695,
15.7002202785958));
#167204=CARTESIAN_POINT('Ctrl Pts',(-20.8386998140563,-18.7238896888305,
15.7008284797941));
#167205=CARTESIAN_POINT('Ctrl Pts',(-20.8367367290434,-18.7065661363465,
15.7018593465851));
#167206=CARTESIAN_POINT('Ctrl Pts',(-20.8359007413786,-18.6995068226344,
15.7022807726844));
#167207=CARTESIAN_POINT('Ctrl Pts',(-20.8342952123103,-18.6865101421559,
15.703059191235));
#167208=CARTESIAN_POINT('Ctrl Pts',(-20.8335360061598,-18.6805715542189,
15.7034158550995));
#167209=CARTESIAN_POINT('Ctrl Pts',(-20.8319166972447,-18.6683185904104,
15.7041538110236));
#167210=CARTESIAN_POINT('Ctrl Pts',(-20.8310532538255,-18.6620047242297,
15.7045352051574));
#167211=CARTESIAN_POINT('Ctrl Pts',(-20.829051087632,-18.6478407310378,
15.70539337289));
#167212=CARTESIAN_POINT('Ctrl Pts',(-20.8278967296628,-18.6399929431577,
15.7058706368674));
#167213=CARTESIAN_POINT('Ctrl Pts',(-20.8248477064104,-18.6200438297961,
15.7070884616442));
#167214=CARTESIAN_POINT('Ctrl Pts',(-20.8228920894939,-18.6079522432944,
15.7078309441352));
#167215=CARTESIAN_POINT('Ctrl Pts',(-20.8108471705794,-18.5373703808585,
15.712190926308));
#167216=CARTESIAN_POINT('Ctrl Pts',(-20.7984074056688,-18.4793131503511,
15.7158825925014));
#167217=CARTESIAN_POINT('Ctrl Pts',(-20.7682273476263,-18.3626357677033,
15.7235218213669));
#167218=CARTESIAN_POINT('Ctrl Pts',(-20.7503497420336,-18.3041081380381,
15.7274702344468));
#167219=CARTESIAN_POINT('Ctrl Pts',(-20.7275382064969,-18.2395763771033,
15.731940929413));
#167220=CARTESIAN_POINT('Ctrl Pts',(-20.7250768450579,-18.2327260841001,
15.7324169989626));
#167221=CARTESIAN_POINT('Ctrl Pts',(-20.7225805680845,-18.2258895922541,
15.7328935628168));
#167222=CARTESIAN_POINT('Origin',(-18.734,-18.952,0.));
#167223=CARTESIAN_POINT('',(-20.7225806455427,-18.225889804387,16.7554729693871));
#167224=CARTESIAN_POINT('',(-20.7225805737622,-18.2258896078036,16.5356516434534));
#167225=CARTESIAN_POINT('',(-20.7225805737622,-18.2258896078036,0.));
#167226=CARTESIAN_POINT('Ctrl Pts',(-20.7225806455427,-18.225889804387,
16.7554729693871));
#167227=CARTESIAN_POINT('Ctrl Pts',(-20.7433304007774,-18.2827166633251,
16.7521870153233));
#167228=CARTESIAN_POINT('Ctrl Pts',(-20.7616464121081,-18.3404387186907,
16.7488940864294));
#167229=CARTESIAN_POINT('Ctrl Pts',(-20.8031161861311,-18.4936521079305,
16.7401351474939));
#167230=CARTESIAN_POINT('Ctrl Pts',(-20.8221382618788,-18.5900612993263,
16.7345999458387));
#167231=CARTESIAN_POINT('Ctrl Pts',(-20.8362368161789,-18.7019907840574,
16.727981337334));
#167232=CARTESIAN_POINT('Ctrl Pts',(-20.8379188844333,-18.7165651876537,
16.7271160006981));
#167233=CARTESIAN_POINT('Ctrl Pts',(-20.8402567486994,-18.7388535287691,
16.7257868384695));
#167234=CARTESIAN_POINT('Ctrl Pts',(-20.841021963568,-18.7465557198488,
16.7253264607647));
#167235=CARTESIAN_POINT('Ctrl Pts',(-20.842281502877,-18.759981493603,16.7245220637299));
#167236=CARTESIAN_POINT('Ctrl Pts',(-20.8427948029376,-18.7657032467542,
16.7241786455911));
#167237=CARTESIAN_POINT('Ctrl Pts',(-20.8438966146525,-18.7785735783429,
16.7234047859348));
#167238=CARTESIAN_POINT('Ctrl Pts',(-20.8444720950107,-18.7857231752158,
16.7229739387381));
#167239=CARTESIAN_POINT('Ctrl Pts',(-20.8459169689109,-18.8048914669959,
16.7218161867558));
#167240=CARTESIAN_POINT('Ctrl Pts',(-20.8467200883861,-18.8169147573708,
16.7210872104599));
#167241=CARTESIAN_POINT('Ctrl Pts',(-20.8498276623859,-18.870285691608,
16.7178385757437));
#167242=CARTESIAN_POINT('Ctrl Pts',(-20.8510211084486,-18.9116865688087,
16.7152844039434));
#167243=CARTESIAN_POINT('Ctrl Pts',(-20.850912165469,-19.1225723337198,
16.7020917815533));
#167244=CARTESIAN_POINT('Ctrl Pts',(-20.8304727788428,-19.2914051854431,
16.6908606080341));
#167245=CARTESIAN_POINT('Ctrl Pts',(-20.7654397479167,-19.5567378280083,
16.6728476439127));
#167246=CARTESIAN_POINT('Ctrl Pts',(-20.7333602044736,-19.6555759962661,
16.6660710908063));
#167247=CARTESIAN_POINT('Ctrl Pts',(-20.6904971169902,-19.7606419972116,
16.6590603002077));
#167248=CARTESIAN_POINT('Ctrl Pts',(-20.6867761538587,-19.769586784111,
16.6584650715421));
#167249=CARTESIAN_POINT('Ctrl Pts',(-20.6811908866164,-19.7827574721508,
16.6575913897736));
#167250=CARTESIAN_POINT('Ctrl Pts',(-20.6793740068196,-19.7870031742334,
16.6573101755078));
#167251=CARTESIAN_POINT('Ctrl Pts',(-20.6761257889957,-19.7945254915889,
16.6568127353112));
#167252=CARTESIAN_POINT('Ctrl Pts',(-20.6747000299203,-19.7978044566008,
16.6565961749707));
#167253=CARTESIAN_POINT('Ctrl Pts',(-20.6716271662102,-19.8048227597676,
16.6561332441046));
#167254=CARTESIAN_POINT('Ctrl Pts',(-20.6699775459862,-19.808560935894,
16.6558870300943));
#167255=CARTESIAN_POINT('Ctrl Pts',(-20.6654189081288,-19.8188107430203,
16.6552128510389));
#167256=CARTESIAN_POINT('Ctrl Pts',(-20.6624877614455,-19.8253125558148,
16.6547862198358));
#167257=CARTESIAN_POINT('Ctrl Pts',(-20.6466515931049,-19.8599714948498,
16.6525168352999));
#167258=CARTESIAN_POINT('Ctrl Pts',(-20.6331619290125,-19.8878592562669,
16.6507079280444));
#167259=CARTESIAN_POINT('Ctrl Pts',(-20.5446480453333,-20.0610448453689,
16.6395212795386));
#167260=CARTESIAN_POINT('Ctrl Pts',(-20.4536052813395,-20.1975508157827,
16.6308787629752));
#167261=CARTESIAN_POINT('Ctrl Pts',(-20.2715339080947,-20.4119803264541,
16.6154836238592));
#167262=CARTESIAN_POINT('Ctrl Pts',(-20.1879784152798,-20.4952091533928,
16.6089133731584));
#167263=CARTESIAN_POINT('Ctrl Pts',(-20.0870076676277,-20.5802701809529,
16.6011790515034));
#167264=CARTESIAN_POINT('Ctrl Pts',(-20.0759772262385,-20.5893730913118,
16.6003368740551));
#167265=CARTESIAN_POINT('Ctrl Pts',(-20.0582778839451,-20.6036805455875,
16.5989894230401));
#167266=CARTESIAN_POINT('Ctrl Pts',(-20.0516684376678,-20.6089581840788,
16.5984870967004));
#167267=CARTESIAN_POINT('Ctrl Pts',(-20.0399575021892,-20.6181949766471,
16.597598456269));
#167268=CARTESIAN_POINT('Ctrl Pts',(-20.0348691637174,-20.6221706844486,
16.597212809302));
#167269=CARTESIAN_POINT('Ctrl Pts',(-20.0243087507026,-20.6303443907801,
16.5964133438653));
#167270=CARTESIAN_POINT('Ctrl Pts',(-20.0188341977554,-20.6345390482035,
16.5959993996052));
#167271=CARTESIAN_POINT('Ctrl Pts',(-20.0047322523664,-20.6452351409896,
16.5949343429442));
#167272=CARTESIAN_POINT('Ctrl Pts',(-19.9960754940778,-20.6516973672864,
16.5942817035537));
#167273=CARTESIAN_POINT('Ctrl Pts',(-19.959764187597,-20.6783732256257,
16.5915487090691));
#167274=CARTESIAN_POINT('Ctrl Pts',(-19.9316718087257,-20.6979794904271,
16.5894450879867));
#167275=CARTESIAN_POINT('Ctrl Pts',(-19.8572712434404,-20.7472645789596,
16.5838981328216));
#167276=CARTESIAN_POINT('Ctrl Pts',(-19.8102625768518,-20.7758342151229,
16.5804165427932));
#167277=CARTESIAN_POINT('Ctrl Pts',(-19.6666536112232,-20.8556263228075,
16.5698575657444));
#167278=CARTESIAN_POINT('Ctrl Pts',(-19.5671477253852,-20.9012299337775,
16.5626317531228));
#167279=CARTESIAN_POINT('Ctrl Pts',(-19.4286088059413,-20.9521690157592,
16.552881044773));
#167280=CARTESIAN_POINT('Ctrl Pts',(-19.392289113875,-20.9644147255279,
16.5503534706963));
#167281=CARTESIAN_POINT('Ctrl Pts',(-19.3246456648601,-20.9851943145759,
16.5457174296647));
#167282=CARTESIAN_POINT('Ctrl Pts',(-19.2934188655449,-20.9940068800373,
16.5436047819984));
#167283=CARTESIAN_POINT('Ctrl Pts',(-19.25610976587,-21.0036158021435,16.5411216843684));
#167284=CARTESIAN_POINT('Ctrl Pts',(-19.2502120930008,-21.0051076648632,
16.5407303765171));
#167285=CARTESIAN_POINT('Ctrl Pts',(-19.201934124693,-21.0170987799747,
16.5375374567557));
#167286=CARTESIAN_POINT('Ctrl Pts',(-19.1592412847681,-21.0263109145861,
16.5347785708004));
#167287=CARTESIAN_POINT('Ctrl Pts',(-19.1088916453316,-21.0355550985196,
16.5316235776351));
#167288=CARTESIAN_POINT('Ctrl Pts',(-19.1014850874102,-21.0368741709515,
16.5311619582455));
#167289=CARTESIAN_POINT('Ctrl Pts',(-19.0895113834967,-21.0389408402356,
16.5304198760706));
#167290=CARTESIAN_POINT('Ctrl Pts',(-19.0849486182727,-21.039712979006,
16.5301380743789));
#167291=CARTESIAN_POINT('Ctrl Pts',(-19.0768549940912,-21.0410553473933,
16.5296399842439));
#167292=CARTESIAN_POINT('Ctrl Pts',(-19.0733251879188,-21.0416315964721,
16.5294233581386));
#167293=CARTESIAN_POINT('Ctrl Pts',(-19.0657655361668,-21.0428460668367,
16.5289607163303));
#167294=CARTESIAN_POINT('Ctrl Pts',(-19.0617353120279,-21.0434815830151,
16.5287148548996));
#167295=CARTESIAN_POINT('Ctrl Pts',(-19.0506819368636,-21.0451918282216,
16.52804263549));
#167296=CARTESIAN_POINT('Ctrl Pts',(-19.0436550991242,-21.0462428707567,
16.5276175984607));
#167297=CARTESIAN_POINT('Ctrl Pts',(-19.0063349687547,-21.051633102683,
16.5253717842882));
#167298=CARTESIAN_POINT('Ctrl Pts',(-18.9759538526256,-21.0553506732712,
16.5235840258274));
#167299=CARTESIAN_POINT('Ctrl Pts',(-18.8841163528689,-21.0645719285763,
16.5182730500866));
#167300=CARTESIAN_POINT('Ctrl Pts',(-18.8224868914983,-21.0680496800947,
16.5148337853914));
#167301=CARTESIAN_POINT('Ctrl Pts',(-18.6143119207719,-21.0706842330412,
16.5033847511416));
#167302=CARTESIAN_POINT('Ctrl Pts',(-18.4680405289909,-21.057330010441,
16.4955930882093));
#167303=CARTESIAN_POINT('Ctrl Pts',(-18.2502318366963,-21.0143674859086,
16.483203073728));
#167304=CARTESIAN_POINT('Ctrl Pts',(-18.1769878617819,-20.9958020841793,
16.4789020525457));
#167305=CARTESIAN_POINT('Ctrl Pts',(-18.092339907895,-20.9694573804946,
16.4737005392247));
#167306=CARTESIAN_POINT('Ctrl Pts',(-18.0798196479728,-20.9654323955079,
16.4729252095672));
#167307=CARTESIAN_POINT('Ctrl Pts',(-18.0595477196723,-20.9587063784519,
16.4716597749045));
#167308=CARTESIAN_POINT('Ctrl Pts',(-18.0517727126453,-20.9560764190143,
16.4711720123531));
#167309=CARTESIAN_POINT('Ctrl Pts',(-18.0379616925817,-20.9513150449416,
16.4703011813339));
#167310=CARTESIAN_POINT('Ctrl Pts',(-18.0319196520133,-20.9492013313395,
16.469918703543));
#167311=CARTESIAN_POINT('Ctrl Pts',(-18.0192156464425,-20.9446922609549,
16.4691112863063));
#167312=CARTESIAN_POINT('Ctrl Pts',(-18.0125559357631,-20.9422908278044,
16.4686861483788));
#167313=CARTESIAN_POINT('Ctrl Pts',(-17.9949886405581,-20.9358564589759,
16.4675596810414));
#167314=CARTESIAN_POINT('Ctrl Pts',(-17.9841021399848,-20.9317670141442,
16.4668564710611));
#167315=CARTESIAN_POINT('Ctrl Pts',(-17.9338560790471,-20.9124185035176,
16.4635865962899));
#167316=CARTESIAN_POINT('Ctrl Pts',(-17.8949270703928,-20.8960749010727,
16.4609837014544));
#167317=CARTESIAN_POINT('Ctrl Pts',(-17.7022848815273,-20.80833354588,16.4477412616152));
#167318=CARTESIAN_POINT('Ctrl Pts',(-17.5570685797906,-20.7198305109251,
16.4365104661703));
#167319=CARTESIAN_POINT('Ctrl Pts',(-17.3424662776604,-20.550777992831,
16.4184972078534));
#167320=CARTESIAN_POINT('Ctrl Pts',(-17.2657722325295,-20.4806495720731,
16.4117200331262));
#167321=CARTESIAN_POINT('Ctrl Pts',(-17.1878748806363,-20.3981258463336,
16.4047086835717));
#167322=CARTESIAN_POINT('Ctrl Pts',(-17.1812733680155,-20.3910353931278,
16.404113455817));
#167323=CARTESIAN_POINT('Ctrl Pts',(-17.1715970514039,-20.3804982858402,
16.4032397751254));
#167324=CARTESIAN_POINT('Ctrl Pts',(-17.1684845883978,-20.3770866020698,
16.4029585610351));
#167325=CARTESIAN_POINT('Ctrl Pts',(-17.1629821591379,-20.3710154079326,
16.4024611210324));
#167326=CARTESIAN_POINT('Ctrl Pts',(-17.1605877441662,-20.3683600030105,
16.4022445607113));
#167327=CARTESIAN_POINT('Ctrl Pts',(-17.1554714956469,-20.3626571007061,
16.401781629758));
#167328=CARTESIAN_POINT('Ctrl Pts',(-17.1527517613888,-20.3596077945813,
16.4015354156416));
#167329=CARTESIAN_POINT('Ctrl Pts',(-17.1453091422223,-20.3512145015766,
16.4008612359966));
#167330=CARTESIAN_POINT('Ctrl Pts',(-17.1406043566029,-20.3458544364128,
16.4004346043137));
#167331=CARTESIAN_POINT('Ctrl Pts',(-17.1156121589638,-20.3170894311429,
16.3981652126395));
#167332=CARTESIAN_POINT('Ctrl Pts',(-17.0958120028952,-20.2932638343221,
16.3963562989776));
#167333=CARTESIAN_POINT('Ctrl Pts',(-16.9748146182204,-20.1409885282248,
16.3851696252664));
#167334=CARTESIAN_POINT('Ctrl Pts',(-16.8882525121577,-20.0015977725196,
16.376527091936));
#167335=CARTESIAN_POINT('Ctrl Pts',(-16.7684483562408,-19.7470847110939,
16.3611319568612));
#167336=CARTESIAN_POINT('Ctrl Pts',(-16.7272828594526,-19.6365684268349,
16.3545617307249));
#167337=CARTESIAN_POINT('Ctrl Pts',(-16.6916599373497,-19.5094411172259,
16.346827436716));
#167338=CARTESIAN_POINT('Ctrl Pts',(-16.6879408231711,-19.4956316405894,
16.3459852595905));
#167339=CARTESIAN_POINT('Ctrl Pts',(-16.6822453265477,-19.47359687357,16.3446378089953));
#167340=CARTESIAN_POINT('Ctrl Pts',(-16.6801777928989,-19.4653954392108,
16.3441354827498));
#167341=CARTESIAN_POINT('Ctrl Pts',(-16.6766185543211,-19.4509110989956,
16.3432468424284));
#167342=CARTESIAN_POINT('Ctrl Pts',(-16.6751063363659,-19.4446333100251,
16.3428611954765));
#167343=CARTESIAN_POINT('Ctrl Pts',(-16.6720384352565,-19.4316363953371,
16.3420617300151));
#167344=CARTESIAN_POINT('Ctrl Pts',(-16.670486819531,-19.4249163969364,
16.3416477857149));
#167345=CARTESIAN_POINT('Ctrl Pts',(-16.6665891812606,-19.4076514089845,
16.3405827288332));
#167346=CARTESIAN_POINT('Ctrl Pts',(-16.6642910076633,-19.3970959224894,
16.3399300892607));
#167347=CARTESIAN_POINT('Ctrl Pts',(-16.655042903979,-19.3529984444207,
16.3371970930156));
#167348=CARTESIAN_POINT('Ctrl Pts',(-16.6488271141355,-19.3193093794526,
16.335093470317));
#167349=CARTESIAN_POINT('Ctrl Pts',(-16.6347687364804,-19.2311796972352,
16.3295465098757));
#167350=CARTESIAN_POINT('Ctrl Pts',(-16.628225824255,-19.1765606947516,
16.3260649160965));
#167351=CARTESIAN_POINT('Ctrl Pts',(-16.6150523778384,-19.0128023052817,
16.31550593184));
#167352=CARTESIAN_POINT('Ctrl Pts',(-16.6147394887864,-18.9033444449292,
16.3082801157851));
#167353=CARTESIAN_POINT('Ctrl Pts',(-16.6317147686931,-18.6760083004113,
16.2932208042183));
#167354=CARTESIAN_POINT('Ctrl Pts',(-16.6504903797373,-18.5585933039911,
16.2854153491064));
#167355=CARTESIAN_POINT('Ctrl Pts',(-16.681299499744,-18.4341194351724,
16.2774951671424));
#167356=CARTESIAN_POINT('Ctrl Pts',(-16.6836490795375,-18.4248940012532,
16.2769103820135));
#167357=CARTESIAN_POINT('Ctrl Pts',(-16.6872224857877,-18.4112488259812,
16.2760490572723));
#167358=CARTESIAN_POINT('Ctrl Pts',(-16.6883985325368,-18.4068168545214,
16.2757698657304));
#167359=CARTESIAN_POINT('Ctrl Pts',(-16.6905163956354,-18.3989389550257,
16.2752746531635));
#167360=CARTESIAN_POINT('Ctrl Pts',(-16.6914525416327,-18.3954915618333,
16.2750583089369));
#167361=CARTESIAN_POINT('Ctrl Pts',(-16.693483760298,-18.3880856949776,
16.2745943351165));
#167362=CARTESIAN_POINT('Ctrl Pts',(-16.6945816242233,-18.3841280451547,
16.274346869938));
#167363=CARTESIAN_POINT('Ctrl Pts',(-16.6976433006485,-18.3732145190731,
16.2736657266126));
#167364=CARTESIAN_POINT('Ctrl Pts',(-16.6996312499662,-18.3662653909507,
16.273233428569));
#167365=CARTESIAN_POINT('Ctrl Pts',(-16.7107070706989,-18.3282851370081,
16.2708777924707));
#167366=CARTESIAN_POINT('Ctrl Pts',(-16.7204699065066,-18.2974533415275,
16.268991421104));
#167367=CARTESIAN_POINT('Ctrl Pts',(-16.7836410857761,-18.1127683304777,
16.2577818114249));
#167368=CARTESIAN_POINT('Ctrl Pts',(-16.8539552330603,-17.9652612904372,
16.2491744108014));
#167369=CARTESIAN_POINT('Ctrl Pts',(-17.0025994125749,-17.728233323449,
16.2338581171959));
#167370=CARTESIAN_POINT('Ctrl Pts',(-17.0727897122348,-17.6345297020076,
16.227332724695));
#167371=CARTESIAN_POINT('Ctrl Pts',(-17.1598314465528,-17.5364129871619,
16.2196488940311));
#167372=CARTESIAN_POINT('Ctrl Pts',(-17.1694229890076,-17.5258190902483,
16.2188073366481));
#167373=CARTESIAN_POINT('Ctrl Pts',(-17.1848587356927,-17.509113369155,
16.217460692462));
#167374=CARTESIAN_POINT('Ctrl Pts',(-17.1906336750816,-17.5029379343191,
16.2169585473031));
#167375=CARTESIAN_POINT('Ctrl Pts',(-17.2008837715803,-17.4921077706464,
16.2160701179424));
#167376=CARTESIAN_POINT('Ctrl Pts',(-17.2053435465578,-17.4874385854138,
16.2156844998494));
#167377=CARTESIAN_POINT('Ctrl Pts',(-17.2146118821266,-17.4778235075864,
16.2148849868044));
#167378=CARTESIAN_POINT('Ctrl Pts',(-17.2194233902501,-17.4728805744747,
16.2144709655322));
#167379=CARTESIAN_POINT('Ctrl Pts',(-17.2318357897996,-17.4602532020903,
16.2134054844155));
#167380=CARTESIAN_POINT('Ctrl Pts',(-17.2394714603043,-17.4526033677739,
16.2127524952305));
#167381=CARTESIAN_POINT('Ctrl Pts',(-17.2715846280124,-17.4209196467429,
16.2100161127028));
#167382=CARTESIAN_POINT('Ctrl Pts',(-17.2965847734587,-17.3974251325252,
16.2079093811543));
#167383=CARTESIAN_POINT('Ctrl Pts',(-17.3632024511578,-17.3378007008676,
16.2023522685208));
#167384=CARTESIAN_POINT('Ctrl Pts',(-17.4056773673499,-17.3026718155528,
16.1988634565686));
#167385=CARTESIAN_POINT('Ctrl Pts',(-17.5364258213347,-17.2028653557094,
16.1882906043449));
#167386=CARTESIAN_POINT('Ctrl Pts',(-17.6283885083299,-17.1433331758317,
16.1810581842581));
#167387=CARTESIAN_POINT('Ctrl Pts',(-17.8286028055045,-17.0347197674754,
16.1660118140119));
#167388=CARTESIAN_POINT('Ctrl Pts',(-17.9372409669876,-16.9870854624434,
16.1582259124908));
#167389=CARTESIAN_POINT('Ctrl Pts',(-18.0583234426079,-16.9456996596702,
16.1503222336106));
#167390=CARTESIAN_POINT('Ctrl Pts',(-18.0673643776012,-16.9426775220053,
16.1497366565087));
#167391=CARTESIAN_POINT('Ctrl Pts',(-18.0807864631423,-16.9382914503205,
16.1488743939089));
#167392=CARTESIAN_POINT('Ctrl Pts',(-18.0851519853102,-16.9368805736297,
16.1485950482683));
#167393=CARTESIAN_POINT('Ctrl Pts',(-18.0929250020887,-16.9343963200008,
16.1480996665727));
#167394=CARTESIAN_POINT('Ctrl Pts',(-18.0963306550094,-16.9333173677835,
16.1478833064619));
#167395=CARTESIAN_POINT('Ctrl Pts',(-18.1036559237867,-16.9310170213546,
16.147419414766));
#167396=CARTESIAN_POINT('Ctrl Pts',(-18.1075763546096,-16.9297984097658,
16.1471720469845));
#167397=CARTESIAN_POINT('Ctrl Pts',(-18.1184013853841,-16.9264681000771,
16.1464914463911));
#167398=CARTESIAN_POINT('Ctrl Pts',(-18.1253133564909,-16.9243802858148,
16.1460595900522));
#167399=CARTESIAN_POINT('Ctrl Pts',(-18.1631324759223,-16.9131675463646,
16.1437108193451));
#167400=CARTESIAN_POINT('Ctrl Pts',(-18.1942360177133,-16.9047133560511,
16.1418306179178));
#167401=CARTESIAN_POINT('Ctrl Pts',(-18.3836962095876,-16.8578350236903,
16.1306206037636));
#167402=CARTESIAN_POINT('Ctrl Pts',(-18.5458760788671,-16.8370860438932,
16.1220085093624));
#167403=CARTESIAN_POINT('Ctrl Pts',(-18.8257588912867,-16.833760147858,
16.1066857054097));
#167404=CARTESIAN_POINT('Ctrl Pts',(-18.9425712162399,-16.8420586397392,
16.1001587624404));
#167405=CARTESIAN_POINT('Ctrl Pts',(-19.072215412372,-16.8621426911253,
16.0924731864519));
#167406=CARTESIAN_POINT('Ctrl Pts',(-19.0863153060788,-16.8644734380583,
16.0916316066258));
#167407=CARTESIAN_POINT('Ctrl Pts',(-19.1087177432724,-16.8684100448933,
16.090284933236));
#167408=CARTESIAN_POINT('Ctrl Pts',(-19.1170362825691,-16.8699232263875,
16.0897827815184));
#167409=CARTESIAN_POINT('Ctrl Pts',(-19.1316910479962,-16.8726797933575,
16.088894344518));
#167410=CARTESIAN_POINT('Ctrl Pts',(-19.1380311038229,-16.8739024187671,
16.0885087253806));
#167411=CARTESIAN_POINT('Ctrl Pts',(-19.1511326109341,-16.8764911544907,
16.087709214063));
#167412=CARTESIAN_POINT('Ctrl Pts',(-19.157893169326,-16.8778613445242,
16.0872951955818));
#167413=CARTESIAN_POINT('Ctrl Pts',(-19.1752291412896,-16.8814631942712,
16.0862297298473));
#167414=CARTESIAN_POINT('Ctrl Pts',(-19.1857942834094,-16.883742826026,
16.0855767533386));
#167415=CARTESIAN_POINT('Ctrl Pts',(-19.2298155706251,-16.8935946549533,
16.0828404936628));
#167416=CARTESIAN_POINT('Ctrl Pts',(-19.2631011082522,-16.90189818653,16.0807338749108));
#167417=CARTESIAN_POINT('Ctrl Pts',(-19.3492891962965,-16.9256377266945,
16.075177130733));
#167418=CARTESIAN_POINT('Ctrl Pts',(-19.4018141917393,-16.9423362862348,
16.0716885807934));
#167419=CARTESIAN_POINT('Ctrl Pts',(-19.6495378507836,-17.0318760899302,
16.0547574511729));
#167420=CARTESIAN_POINT('Ctrl Pts',(-19.8338998364072,-17.1312054412726,
16.0405669763651));
#167421=CARTESIAN_POINT('Ctrl Pts',(-20.0044080120687,-17.2585499789393,
16.0271505076349));
#167422=CARTESIAN_POINT('Ctrl Pts',(-20.0080261722787,-17.2612703338487,
16.0268657280972));
#167423=CARTESIAN_POINT('Ctrl Pts',(-20.0280040217407,-17.2763914514997,
16.025292962427));
#167424=CARTESIAN_POINT('Ctrl Pts',(-20.0441920761446,-17.2890185773859,
16.0240172720375));
#167425=CARTESIAN_POINT('Ctrl Pts',(-20.0652189659571,-17.3059177980897,
16.0223613761366));
#167426=CARTESIAN_POINT('Ctrl Pts',(-20.0702249728066,-17.3099788748926,
16.0219672316426));
#167427=CARTESIAN_POINT('Ctrl Pts',(-20.0782557868953,-17.3165548460233,
16.0213351779903));
#167428=CARTESIAN_POINT('Ctrl Pts',(-20.0812922245914,-17.3190553792589,
16.0210962568669));
#167429=CARTESIAN_POINT('Ctrl Pts',(-20.0869640811617,-17.323752793223,
16.0206501052632));
#167430=CARTESIAN_POINT('Ctrl Pts',(-20.0896011292765,-17.3259476177834,
16.0204427323188));
#167431=CARTESIAN_POINT('Ctrl Pts',(-20.0958375106931,-17.331163895237,
16.0199524288521));
#167432=CARTESIAN_POINT('Ctrl Pts',(-20.0994321632624,-17.334190959187,
16.0196699071926));
#167433=CARTESIAN_POINT('Ctrl Pts',(-20.1106650807128,-17.3437143291432,
16.0187872291092));
#167434=CARTESIAN_POINT('Ctrl Pts',(-20.1182674188441,-17.3502530582034,
16.0181900923124));
#167435=CARTESIAN_POINT('Ctrl Pts',(-20.1360932561222,-17.3658066717296,
16.0167897424049));
#167436=CARTESIAN_POINT('Ctrl Pts',(-20.1462768332242,-17.3748668604227,
16.0159895953197));
#167437=CARTESIAN_POINT('Ctrl Pts',(-20.1816926502187,-17.4069939564975,
16.0132034065174));
#167438=CARTESIAN_POINT('Ctrl Pts',(-20.2064541365772,-17.4305741061277,
16.0112490691357));
#167439=CARTESIAN_POINT('Ctrl Pts',(-20.284326716011,-17.50841442696,16.0050399557774));
#167440=CARTESIAN_POINT('Ctrl Pts',(-20.3350960491686,-17.5649365441214,
16.0008919511948));
#167441=CARTESIAN_POINT('Ctrl Pts',(-20.4906343550071,-17.7580482000638,
15.9874071572346));
#167442=CARTESIAN_POINT('Ctrl Pts',(-20.5818013803714,-17.9046660609108,
15.9781419429746));
#167443=CARTESIAN_POINT('Ctrl Pts',(-20.6640048012645,-18.0817643148415,
15.9667991612902));
#167444=CARTESIAN_POINT('Ctrl Pts',(-20.6734378070351,-18.1029949290666,
15.965438375539));
#167445=CARTESIAN_POINT('Ctrl Pts',(-20.6862667106885,-18.1331986957681,
15.9634992255069));
#167446=CARTESIAN_POINT('Ctrl Pts',(-20.6899541444026,-18.1420467508086,
15.9629307780299));
#167447=CARTESIAN_POINT('Ctrl Pts',(-20.6958419130385,-18.1564492490118,
15.9620047434131));
#167448=CARTESIAN_POINT('Ctrl Pts',(-20.6980790762592,-18.1619885632303,
15.961648406972));
#167449=CARTESIAN_POINT('Ctrl Pts',(-20.7027082004979,-18.1735916803545,
15.9609015928601));
#167450=CARTESIAN_POINT('Ctrl Pts',(-20.7050956576965,-18.1796572020561,
15.9605109679891));
#167451=CARTESIAN_POINT('Ctrl Pts',(-20.7107003736708,-18.1940916794411,
15.9595807886435));
#167452=CARTESIAN_POINT('Ctrl Pts',(-20.7138925340841,-18.2024701878809,
15.9590403984714));
#167453=CARTESIAN_POINT('Ctrl Pts',(-20.7189000460753,-18.2158686938571,
15.9581754212387));
#167454=CARTESIAN_POINT('Ctrl Pts',(-20.7207498043567,-18.2208757249084,
15.95785199894));
#167455=CARTESIAN_POINT('Ctrl Pts',(-20.7225805738037,-18.2258896079172,
15.9575279467182));
#167456=CARTESIAN_POINT('Ctrl Pts',(-20.7225805680844,-18.2258895922541,
15.7328935628168));
#167457=CARTESIAN_POINT('Ctrl Pts',(-20.6693404889608,-18.0800823077706,
15.7430576181593));
#167458=CARTESIAN_POINT('Ctrl Pts',(-20.600219906329,-17.9405553341241,
15.7534914468738));
#167459=CARTESIAN_POINT('Ctrl Pts',(-20.4987970870316,-17.7822775194804,
15.7654387928763));
#167460=CARTESIAN_POINT('Ctrl Pts',(-20.4805077342581,-17.7551414254491,
15.7674896854294));
#167461=CARTESIAN_POINT('Ctrl Pts',(-20.4574030229023,-17.7225189551059,
15.7699479745011));
#167462=CARTESIAN_POINT('Ctrl Pts',(-20.4531800205688,-17.71662083574,15.7703921327795));
#167463=CARTESIAN_POINT('Ctrl Pts',(-20.4465152606251,-17.7074127602526,
15.7710849267591));
#167464=CARTESIAN_POINT('Ctrl Pts',(-20.444094078235,-17.7040880802449,
15.7713349400436));
#167465=CARTESIAN_POINT('Ctrl Pts',(-20.4395523386009,-17.6978895680709,
15.771800790781));
#167466=CARTESIAN_POINT('Ctrl Pts',(-20.4374342212101,-17.6950140774759,
15.7720167848616));
#167467=CARTESIAN_POINT('Ctrl Pts',(-20.4325851774586,-17.6884659322428,
15.7725084082));
#167468=CARTESIAN_POINT('Ctrl Pts',(-20.4298496174517,-17.6847967718805,
15.7727837098655));
#167469=CARTESIAN_POINT('Ctrl Pts',(-20.4214139000893,-17.6735583258191,
15.7736265114171));
#167470=CARTESIAN_POINT('Ctrl Pts',(-20.4156747152556,-17.6660182955739,
15.7741913527461));
#167471=CARTESIAN_POINT('Ctrl Pts',(-20.3358231113844,-17.5625595777808,
15.7819371900118));
#167472=CARTESIAN_POINT('Ctrl Pts',(-20.2536450104188,-17.4731255568374,
15.7885861201467));
#167473=CARTESIAN_POINT('Ctrl Pts',(-20.0843244631099,-17.3179664642329,
15.8010832541351));
#167474=CARTESIAN_POINT('Ctrl Pts',(-19.9988904749386,-17.2509730015323,
15.8069253952696));
#167475=CARTESIAN_POINT('Ctrl Pts',(-19.8637962840653,-17.1608653170644,
15.8159630588426));
#167476=CARTESIAN_POINT('Ctrl Pts',(-19.817760545941,-17.1326414419455,
15.8190095450046));
#167477=CARTESIAN_POINT('Ctrl Pts',(-19.7511164034378,-17.095210388649,
15.8234090042272));
#167478=CARTESIAN_POINT('Ctrl Pts',(-19.7313607677121,-17.084524462379,
15.8247117570074));
#167479=CARTESIAN_POINT('Ctrl Pts',(-19.6962617628501,-17.0662550354213,
15.82702619618));
#167480=CARTESIAN_POINT('Ctrl Pts',(-19.6809892769589,-17.0585393969076,
15.8280332281916));
#167481=CARTESIAN_POINT('Ctrl Pts',(-19.6582661738927,-17.0474034015377,
15.8295321841298));
#167482=CARTESIAN_POINT('Ctrl Pts',(-19.6508862813413,-17.0438397060831,
15.8300191058044));
#167483=CARTESIAN_POINT('Ctrl Pts',(-19.6379544133566,-17.0376873447261,
15.8308725939925));
#167484=CARTESIAN_POINT('Ctrl Pts',(-19.6324115153633,-17.0350797430739,
15.8312384983682));
#167485=CARTESIAN_POINT('Ctrl Pts',(-19.6213453955741,-17.0299323359772,
15.8319692000979));
#167486=CARTESIAN_POINT('Ctrl Pts',(-19.6158223956264,-17.02739219125,15.8323339813512));
#167487=CARTESIAN_POINT('Ctrl Pts',(-19.6025844323973,-17.021372715966,
15.8332085796982));
#167488=CARTESIAN_POINT('Ctrl Pts',(-19.5948594403423,-17.0179158118689,
15.8337191620677));
#167489=CARTESIAN_POINT('Ctrl Pts',(-19.5668565065813,-17.0055856124753,
15.8355709046529));
#167490=CARTESIAN_POINT('Ctrl Pts',(-19.5464609881557,-16.9969843957482,
15.8369212966272));
#167491=CARTESIAN_POINT('Ctrl Pts',(-19.3540550539053,-16.9193735591264,
15.8496805843615));
#167492=CARTESIAN_POINT('Ctrl Pts',(-19.1738451659808,-16.8729263471608,
15.8618862752345));
#167493=CARTESIAN_POINT('Ctrl Pts',(-18.9102072121805,-16.8408174010051,
15.8794212657179));
#167494=CARTESIAN_POINT('Ctrl Pts',(-18.8299787501099,-16.8356515527881,
15.8846992286326));
#167495=CARTESIAN_POINT('Ctrl Pts',(-18.7135698354324,-16.8347911808613,
15.8921203730578));
#167496=CARTESIAN_POINT('Ctrl Pts',(-18.6774899759871,-16.8354467754887,
15.8943870852074));
#167497=CARTESIAN_POINT('Ctrl Pts',(-18.633980135916,-16.8373509002736,
15.8970664865295));
#167498=CARTESIAN_POINT('Ctrl Pts',(-18.6265197812475,-16.8377169549504,
15.8975239812815));
#167499=CARTESIAN_POINT('Ctrl Pts',(-18.6149075998526,-16.8383483481803,
15.8982329183928));
#167500=CARTESIAN_POINT('Ctrl Pts',(-18.6107544394904,-16.8385864490083,
15.8984858435178));
#167501=CARTESIAN_POINT('Ctrl Pts',(-18.6030426460603,-16.8390513763321,
15.8989542828912));
#167502=CARTESIAN_POINT('Ctrl Pts',(-18.5994839178959,-16.8392749495632,
15.8991699711456));
#167503=CARTESIAN_POINT('Ctrl Pts',(-18.5914257708345,-16.8398016369341,
15.8996572865141));
#167504=CARTESIAN_POINT('Ctrl Pts',(-18.586926757062,-16.8401101359595,
15.8999286086305));
#167505=CARTESIAN_POINT('Ctrl Pts',(-18.575314335671,-16.8409436920978,
15.9006270478957));
#167506=CARTESIAN_POINT('Ctrl Pts',(-18.5682024680538,-16.8414903324418,
15.9010529837413));
#167507=CARTESIAN_POINT('Ctrl Pts',(-18.5245759179977,-16.8450654887221,
15.9036554211107));
#167508=CARTESIAN_POINT('Ctrl Pts',(-18.4881397919416,-16.8490058007657,
15.905784243566));
#167509=CARTESIAN_POINT('Ctrl Pts',(-18.2827363879426,-16.8766308252548,
15.9176236651224));
#167510=CARTESIAN_POINT('Ctrl Pts',(-18.1170048105963,-16.9197290810761,
15.9266000128124));
#167511=CARTESIAN_POINT('Ctrl Pts',(-17.8695282265188,-17.0171960535051,
15.941231328725));
#167512=CARTESIAN_POINT('Ctrl Pts',(-17.783295613102,-17.0580792365382,
15.9465768614697));
#167513=CARTESIAN_POINT('Ctrl Pts',(-17.6814560607314,-17.1150738845568,
15.9533725383239));
#167514=CARTESIAN_POINT('Ctrl Pts',(-17.6629550070717,-17.125799334274,
15.9546273284147));
#167515=CARTESIAN_POINT('Ctrl Pts',(-17.6368957528842,-17.1414386433616,
15.9564251174629));
#167516=CARTESIAN_POINT('Ctrl Pts',(-17.6292011797927,-17.1461235595312,
15.9569597801513));
#167517=CARTESIAN_POINT('Ctrl Pts',(-17.6159843405472,-17.1542868480853,
15.9578848880821));
#167518=CARTESIAN_POINT('Ctrl Pts',(-17.6104477852283,-17.1577419331212,
15.9582744725098));
#167519=CARTESIAN_POINT('Ctrl Pts',(-17.5998814575152,-17.1644039287878,
15.9590219656223));
#167520=CARTESIAN_POINT('Ctrl Pts',(-17.5948490827513,-17.1676066104076,
15.9593797148631));
#167521=CARTESIAN_POINT('Ctrl Pts',(-17.5818067783103,-17.1759845939957,
15.9603114683245));
#167522=CARTESIAN_POINT('Ctrl Pts',(-17.5738182287436,-17.181192784219,
15.9608866963878));
#167523=CARTESIAN_POINT('Ctrl Pts',(-17.546740597358,-17.1991081118468,
15.9628520900761));
#167524=CARTESIAN_POINT('Ctrl Pts',(-17.5278234312205,-17.2120710127303,
15.9642518475003));
#167525=CARTESIAN_POINT('Ctrl Pts',(-17.3653109714664,-17.327355942597,
15.9765153748533));
#167526=CARTESIAN_POINT('Ctrl Pts',(-17.2348351460839,-17.4469222779745,
15.9880903961454));
#167527=CARTESIAN_POINT('Ctrl Pts',(-17.0647462974219,-17.647104803255,
16.0054455463183));
#167528=CARTESIAN_POINT('Ctrl Pts',(-17.0128643256578,-17.7163409489386,
16.0111404585931));
#167529=CARTESIAN_POINT('Ctrl Pts',(-16.9446526771664,-17.8200350665684,
16.0190638518097));
#167530=CARTESIAN_POINT('Ctrl Pts',(-16.9247896830059,-17.8520605076755,
16.021433516982));
#167531=CARTESIAN_POINT('Ctrl Pts',(-16.9019773457206,-17.8911328085888,
16.0242176105003));
#167532=CARTESIAN_POINT('Ctrl Pts',(-16.8981988637378,-17.8976848688987,
16.0246809407275));
#167533=CARTESIAN_POINT('Ctrl Pts',(-16.892386545359,-17.9078896803595,
16.0253969321961));
#167534=CARTESIAN_POINT('Ctrl Pts',(-16.8903283219204,-17.911528366538,
16.0256511232538));
#167535=CARTESIAN_POINT('Ctrl Pts',(-16.886535415185,-17.918280352754,16.0261207212314));
#167536=CARTESIAN_POINT('Ctrl Pts',(-16.8847978302417,-17.9213919091592,
16.0263363096318));
#167537=CARTESIAN_POINT('Ctrl Pts',(-16.880892563893,-17.9284268851611,
16.0268219028805));
#167538=CARTESIAN_POINT('Ctrl Pts',(-16.8787294867131,-17.9323527989771,
16.0270916119162));
#167539=CARTESIAN_POINT('Ctrl Pts',(-16.8723969817171,-17.9439329523265,
16.0278834921752));
#167540=CARTESIAN_POINT('Ctrl Pts',(-16.868262278401,-17.9516062123351,
16.0284035013328));
#167541=CARTESIAN_POINT('Ctrl Pts',(-16.8391906225886,-18.0063651315831,
16.0320826491193));
#167542=CARTESIAN_POINT('Ctrl Pts',(-16.8159894888871,-18.0543560969524,
16.0351406523154));
#167543=CARTESIAN_POINT('Ctrl Pts',(-16.7878975794551,-18.1185399500332,
16.039081030343));
#167544=CARTESIAN_POINT('Ctrl Pts',(-16.7813556003007,-18.1339840128234,
16.0400180910657));
#167545=CARTESIAN_POINT('Ctrl Pts',(-16.7185790792292,-18.2872301580459,
16.0492220961055));
#167546=CARTESIAN_POINT('Ctrl Pts',(-16.6768402139197,-18.4305236918782,
16.0571116269683));
#167547=CARTESIAN_POINT('Ctrl Pts',(-16.6395590291366,-18.6376689096515,
16.0687567174571));
#167548=CARTESIAN_POINT('Ctrl Pts',(-16.631297263296,-18.6987661894777,
16.0722153770887));
#167549=CARTESIAN_POINT('Ctrl Pts',(-16.6223427137143,-18.7971616116903,
16.0778857802934));
#167550=CARTESIAN_POINT('Ctrl Pts',(-16.6199491887369,-18.8342700529912,
16.0800466926872));
#167551=CARTESIAN_POINT('Ctrl Pts',(-16.6181105876072,-18.8825392484015,
16.0828941370441));
#167552=CARTESIAN_POINT('Ctrl Pts',(-16.6177747445232,-18.8936607985675,
16.0835527146772));
#167553=CARTESIAN_POINT('Ctrl Pts',(-16.6173711819886,-18.9117507508806,
16.0846282065509));
#167554=CARTESIAN_POINT('Ctrl Pts',(-16.6172501679848,-18.9187178400606,
16.0850434465598));
#167555=CARTESIAN_POINT('Ctrl Pts',(-16.6170836099393,-18.9321163066294,
16.0858440276361));
#167556=CARTESIAN_POINT('Ctrl Pts',(-16.6170329728605,-18.9385475519692,
16.086229204508));
#167557=CARTESIAN_POINT('Ctrl Pts',(-16.6169841377923,-18.9532721511588,
16.0871131832957));
#167558=CARTESIAN_POINT('Ctrl Pts',(-16.6170053663742,-18.9615654247404,
16.0876125887117));
#167559=CARTESIAN_POINT('Ctrl Pts',(-16.6171912048053,-18.9835947699358,
16.0889433004205));
#167560=CARTESIAN_POINT('Ctrl Pts',(-16.6174407822385,-18.9973295560186,
16.0897772527229));
#167561=CARTESIAN_POINT('Ctrl Pts',(-16.6203578225619,-19.1018486626708,
16.0961570487287));
#167562=CARTESIAN_POINT('Ctrl Pts',(-16.6287309930167,-19.1923674174292,
16.1018814117833));
#167563=CARTESIAN_POINT('Ctrl Pts',(-16.6648011226226,-19.4208919264391,
16.1168225464823));
#167564=CARTESIAN_POINT('Ctrl Pts',(-16.700485727514,-19.5571928642288,
16.1262165228961));
#167565=CARTESIAN_POINT('Ctrl Pts',(-16.7682471058372,-19.739676349936,
16.1389575964096));
#167566=CARTESIAN_POINT('Ctrl Pts',(-16.7890284005296,-19.7896781894948,
16.1424627236111));
#167567=CARTESIAN_POINT('Ctrl Pts',(-16.8234687220353,-19.8643309967244,
16.1476642188366));
#167568=CARTESIAN_POINT('Ctrl Pts',(-16.8357395311062,-19.889595318648,
16.1494187191127));
#167569=CARTESIAN_POINT('Ctrl Pts',(-16.8516528118022,-19.9207651072571,
16.1515692437521));
#167570=CARTESIAN_POINT('Ctrl Pts',(-16.8548257160725,-19.9269055254869,
16.1519922022534));
#167571=CARTESIAN_POINT('Ctrl Pts',(-16.8598995416166,-19.9366079274268,
16.1526592814996));
#167572=CARTESIAN_POINT('Ctrl Pts',(-16.8617806452694,-19.9401801390771,
16.1529046193221));
#167573=CARTESIAN_POINT('Ctrl Pts',(-16.8653513822066,-19.9469141644755,
16.1533665741894));
#167574=CARTESIAN_POINT('Ctrl Pts',(-16.8670388066997,-19.9500770282594,
16.1535833193056));
#167575=CARTESIAN_POINT('Ctrl Pts',(-16.8709199733089,-19.9573075008329,
16.1540783098381));
#167576=CARTESIAN_POINT('Ctrl Pts',(-16.8731190036609,-19.9613722184989,
16.1543562153446));
#167577=CARTESIAN_POINT('Ctrl Pts',(-16.879002574489,-19.972162910879,16.155093103112));
#167578=CARTESIAN_POINT('Ctrl Pts',(-16.8827104212753,-19.9788761917194,
16.1555506412396));
#167579=CARTESIAN_POINT('Ctrl Pts',(-16.909226066583,-20.0262739380936,
16.1587756194034));
#167580=CARTESIAN_POINT('Ctrl Pts',(-16.9333382691052,-20.0662183091007,
16.1614653709725));
#167581=CARTESIAN_POINT('Ctrl Pts',(-16.9612209659845,-20.1091361318867,
16.164360546137));
#167582=CARTESIAN_POINT('Ctrl Pts',(-16.9637017233245,-20.1129278802964,
16.1646163768893));
#167583=CARTESIAN_POINT('Ctrl Pts',(-16.9790315977765,-20.1361956426712,
16.1661867222183));
#167584=CARTESIAN_POINT('Ctrl Pts',(-16.9921901196731,-20.1554665800866,
16.1674893203714));
#167585=CARTESIAN_POINT('Ctrl Pts',(-17.0319413225092,-20.2116649217534,
16.1713057961291));
#167586=CARTESIAN_POINT('Ctrl Pts',(-17.0594094141591,-20.2479575840421,
16.1737938546244));
#167587=CARTESIAN_POINT('Ctrl Pts',(-17.1567932397521,-20.3683561853195,
16.182224685891));
#167588=CARTESIAN_POINT('Ctrl Pts',(-17.232043158185,-20.447918035758,16.1881126943056));
#167589=CARTESIAN_POINT('Ctrl Pts',(-17.353949655852,-20.5582960325788,
16.197256840454));
#167590=CARTESIAN_POINT('Ctrl Pts',(-17.3962267946189,-20.5936723492566,
16.20036424792));
#167591=CARTESIAN_POINT('Ctrl Pts',(-17.4669834775263,-20.6483298863517,
16.2055080947614));
#167592=CARTESIAN_POINT('Ctrl Pts',(-17.4946377878849,-20.6686383026581,
16.2075051497761));
#167593=CARTESIAN_POINT('Ctrl Pts',(-17.5316371049999,-20.6944492242487,
16.2101657318742));
#167594=CARTESIAN_POINT('Ctrl Pts',(-17.5405490926554,-20.7005653420898,
16.2108057320983));
#167595=CARTESIAN_POINT('Ctrl Pts',(-17.5552247318944,-20.7104724768369,
16.2118584314054));
#167596=CARTESIAN_POINT('Ctrl Pts',(-17.5609608381677,-20.7143040905492,
16.2122695892469));
#167597=CARTESIAN_POINT('Ctrl Pts',(-17.5721021383834,-20.7216677795498,
16.2130676568961));
#167598=CARTESIAN_POINT('Ctrl Pts',(-17.5775049724133,-20.7252032992696,
16.2134544313362));
#167599=CARTESIAN_POINT('Ctrl Pts',(-17.5900196128839,-20.7333111343143,
16.2143498149645));
#167600=CARTESIAN_POINT('Ctrl Pts',(-17.5971427696027,-20.7378656494239,
16.214859080305));
#167601=CARTESIAN_POINT('Ctrl Pts',(-17.616378334742,-20.7500030651019,
16.2162334099759));
#167602=CARTESIAN_POINT('Ctrl Pts',(-17.6285403941042,-20.757506093256,
16.2171014025143));
#167603=CARTESIAN_POINT('Ctrl Pts',(-17.7408543730624,-20.8252347014787,
16.2251097131299));
#167604=CARTESIAN_POINT('Ctrl Pts',(-17.8457401892452,-20.8771839345009,
16.2325518997681));
#167605=CARTESIAN_POINT('Ctrl Pts',(-18.105691032488,-20.9801545905997,
16.2508154736347));
#167606=CARTESIAN_POINT('Ctrl Pts',(-18.2634255268701,-21.0224451085997,
16.2617770366288));
#167607=CARTESIAN_POINT('Ctrl Pts',(-18.4565507487976,-21.0509912109393,
16.2741813302676));
#167608=CARTESIAN_POINT('Ctrl Pts',(-18.4887618004647,-21.0549980226765,
16.2762152558618));
#167609=CARTESIAN_POINT('Ctrl Pts',(-18.5282533591424,-21.0589906685718,
16.2786560612136));
#167610=CARTESIAN_POINT('Ctrl Pts',(-18.5354563245833,-21.0596816102314,
16.2790991018273));
#167611=CARTESIAN_POINT('Ctrl Pts',(-18.5467548382939,-21.0607069810728,
16.2797905416686));
#167612=CARTESIAN_POINT('Ctrl Pts',(-18.5508479795884,-21.0610664334463,
16.2800403098128));
#167613=CARTESIAN_POINT('Ctrl Pts',(-18.5585013851382,-21.0617160935517,
16.2805059478559));
#167614=CARTESIAN_POINT('Ctrl Pts',(-18.5620612980682,-21.0620092042967,
16.2807219729064));
#167615=CARTESIAN_POINT('Ctrl Pts',(-18.5701900823374,-21.0626577910543,
16.2812139827468));
#167616=CARTESIAN_POINT('Ctrl Pts',(-18.5747593678951,-21.0630074424445,
16.2814896379402));
#167617=CARTESIAN_POINT('Ctrl Pts',(-18.5888102154943,-21.0640367627134,
16.2823345988338));
#167618=CARTESIAN_POINT('Ctrl Pts',(-18.5982953992801,-21.0646674204766,
16.2829012261454));
#167619=CARTESIAN_POINT('Ctrl Pts',(-18.6836895437452,-21.0697676819452,
16.2879711442723));
#167620=CARTESIAN_POINT('Ctrl Pts',(-18.759792488342,-21.070208786245,16.2922672311556));
#167621=CARTESIAN_POINT('Ctrl Pts',(-18.8781838246555,-21.0645112577357,
16.2988268320853));
#167622=CARTESIAN_POINT('Ctrl Pts',(-18.9205358367219,-21.0611935314556,
16.3011484604701));
#167623=CARTESIAN_POINT('Ctrl Pts',(-19.0714391604339,-21.0447910662302,
16.3094125077734));
#167624=CARTESIAN_POINT('Ctrl Pts',(-19.1790386628083,-21.0245779443096,
16.3152990895486));
#167625=CARTESIAN_POINT('Ctrl Pts',(-19.3377693422375,-20.9818237867634,
16.3244399190603));
#167626=CARTESIAN_POINT('Ctrl Pts',(-19.3903645828794,-20.9654316263566,
16.3275454255471));
#167627=CARTESIAN_POINT('Ctrl Pts',(-19.4745732360926,-20.9355362720992,
16.3326864061115));
#167628=CARTESIAN_POINT('Ctrl Pts',(-19.506603093924,-20.9232810869314,
16.3346825533624));
#167629=CARTESIAN_POINT('Ctrl Pts',(-19.5483165348401,-20.9061479913124,
16.3373420974504));
#167630=CARTESIAN_POINT('Ctrl Pts',(-19.5582814103397,-20.901965625563,
16.3379819908532));
#167631=CARTESIAN_POINT('Ctrl Pts',(-19.5745533211271,-20.8949891130161,
16.3390345592115));
#167632=CARTESIAN_POINT('Ctrl Pts',(-19.5808795728355,-20.8922400795622,
16.3394456936781));
#167633=CARTESIAN_POINT('Ctrl Pts',(-19.5931016139735,-20.8868579042829,
16.3402437479494));
#167634=CARTESIAN_POINT('Ctrl Pts',(-19.5989990200743,-20.8842286062305,
16.3406305325559));
#167635=CARTESIAN_POINT('Ctrl Pts',(-19.6125913968172,-20.8780938859456,
16.3415259863345));
#167636=CARTESIAN_POINT('Ctrl Pts',(-19.620277539638,-20.8745692756129,
16.3420353119828));
#167637=CARTESIAN_POINT('Ctrl Pts',(-19.6408989794062,-20.8649630282152,
16.3434099099331));
#167638=CARTESIAN_POINT('Ctrl Pts',(-19.6537939665719,-20.8587963576363,
16.3442781122221));
#167639=CARTESIAN_POINT('Ctrl Pts',(-19.7717737012449,-20.8009005932817,
16.3523026300373));
#167640=CARTESIAN_POINT('Ctrl Pts',(-19.8724412996336,-20.7406730294043,
16.3597622333303));
#167641=CARTESIAN_POINT('Ctrl Pts',(-20.1005658692126,-20.5771018974074,
16.3780997130634));
#167642=CARTESIAN_POINT('Ctrl Pts',(-20.222027613262,-20.4666724019441,
16.3891199844154));
#167643=CARTESIAN_POINT('Ctrl Pts',(-20.3502424320361,-20.3196401927744,
16.4015038056873));
#167644=CARTESIAN_POINT('Ctrl Pts',(-20.3703947119184,-20.2954626485046,
16.403474702757));
#167645=CARTESIAN_POINT('Ctrl Pts',(-20.3944666551621,-20.2652367863771,
16.4058504237192));
#167646=CARTESIAN_POINT('Ctrl Pts',(-20.3989032864566,-20.2596075176184,
16.4062892167495));
#167647=CARTESIAN_POINT('Ctrl Pts',(-20.4058289727061,-20.2507277023311,
16.4069755086302));
#167648=CARTESIAN_POINT('Ctrl Pts',(-20.4083372859219,-20.2474923436321,
16.407224343668));
#167649=CARTESIAN_POINT('Ctrl Pts',(-20.4130180216304,-20.2414185738344,
16.407689180096));
#167650=CARTESIAN_POINT('Ctrl Pts',(-20.4151926158865,-20.2385819694111,
16.4079053309998));
#167651=CARTESIAN_POINT('Ctrl Pts',(-20.4201529718949,-20.2320774852705,
16.4083988484328));
#167652=CARTESIAN_POINT('Ctrl Pts',(-20.4229339498758,-20.2284060195732,
16.4086758775802));
#167653=CARTESIAN_POINT('Ctrl Pts',(-20.4301820138803,-20.2187719141843,
16.4093988859359));
#167654=CARTESIAN_POINT('Ctrl Pts',(-20.4346296891585,-20.2127946584717,
16.4098435411797));
#167655=CARTESIAN_POINT('Ctrl Pts',(-20.4640847617239,-20.172770360006,
16.412795880125));
#167656=CARTESIAN_POINT('Ctrl Pts',(-20.4881016525195,-20.1380023128013,
16.4152399558393));
#167657=CARTESIAN_POINT('Ctrl Pts',(-20.5515193138918,-20.0400504068208,
16.4218683294491));
#167658=CARTESIAN_POINT('Ctrl Pts',(-20.5886539074199,-19.9754698403651,
16.4259560558961));
#167659=CARTESIAN_POINT('Ctrl Pts',(-20.6728522487848,-19.8093443013035,
16.4361043156865));
#167660=CARTESIAN_POINT('Ctrl Pts',(-20.7154134942979,-19.7057818601762,
16.4421169431856));
#167661=CARTESIAN_POINT('Ctrl Pts',(-20.7754133653133,-19.5189637878021,
16.4530200566841));
#167662=CARTESIAN_POINT('Ctrl Pts',(-20.7963949740725,-19.4371195748214,
16.4578124645552));
#167663=CARTESIAN_POINT('Ctrl Pts',(-20.8151326638564,-19.3403009459394,
16.46360140908));
#167664=CARTESIAN_POINT('Ctrl Pts',(-20.8176912864146,-19.326327927584,
16.4644396207964));
#167665=CARTESIAN_POINT('Ctrl Pts',(-20.8214097413267,-19.3048001825602,
16.4657356371529));
#167666=CARTESIAN_POINT('Ctrl Pts',(-20.8226696398739,-19.2972629869016,
16.4661902581937));
#167667=CARTESIAN_POINT('Ctrl Pts',(-20.8248931361382,-19.2835034506971,
16.4670218343697));
#167668=CARTESIAN_POINT('Ctrl Pts',(-20.8258698386487,-19.2772832940697,
16.467398368603));
#167669=CARTESIAN_POINT('Ctrl Pts',(-20.8279419770617,-19.2636914154738,
16.4682225180916));
#167670=CARTESIAN_POINT('Ctrl Pts',(-20.8290262606143,-19.2563181015063,
16.4686704816853));
#167671=CARTESIAN_POINT('Ctrl Pts',(-20.8318905540241,-19.2360992748401,
16.4699013512523));
#167672=CARTESIAN_POINT('Ctrl Pts',(-20.8335914772361,-19.2232430489611,
16.4706867456919));
#167673=CARTESIAN_POINT('Ctrl Pts',(-20.8416314801174,-19.1578589077599,
16.4746955887798));
#167674=CARTESIAN_POINT('Ctrl Pts',(-20.846117415472,-19.1051260510563,
16.4779768670436));
#167675=CARTESIAN_POINT('Ctrl Pts',(-20.8502336389003,-19.018329912382,
16.4834601303997));
#167676=CARTESIAN_POINT('Ctrl Pts',(-20.8510257893228,-18.9843434163513,
16.4856276880682));
#167677=CARTESIAN_POINT('Ctrl Pts',(-20.8508977919258,-18.8197312346676,
16.4962189028986));
#167678=CARTESIAN_POINT('Ctrl Pts',(-20.8387067143781,-18.6894054886347,
16.5049104438664));
#167679=CARTESIAN_POINT('Ctrl Pts',(-20.7970384719494,-18.4676530630201,
16.5197603527283));
#167680=CARTESIAN_POINT('Ctrl Pts',(-20.7732180773672,-18.3755335280661,
16.525940140316));
#167681=CARTESIAN_POINT('Ctrl Pts',(-20.7402342466764,-18.2761250472743,
16.5324112063177));
#167682=CARTESIAN_POINT('Ctrl Pts',(-20.7371210647758,-18.2669534232681,
16.5330062931116));
#167683=CARTESIAN_POINT('Ctrl Pts',(-20.7324307947245,-18.2534409967208,
16.5338798071661));
#167684=CARTESIAN_POINT('Ctrl Pts',(-20.7309023230061,-18.2490836211387,
16.534160994092));
#167685=CARTESIAN_POINT('Ctrl Pts',(-20.728165063312,-18.2413612139805,
16.534658404075));
#167686=CARTESIAN_POINT('Ctrl Pts',(-20.7269619965586,-18.2379942122916,
16.5348749613903));
#167687=CARTESIAN_POINT('Ctrl Pts',(-20.7247001831083,-18.2317143719838,
16.5352782673501));
#167688=CARTESIAN_POINT('Ctrl Pts',(-20.7236435792586,-18.2288008346675,
16.5354651435967));
#167689=CARTESIAN_POINT('Ctrl Pts',(-20.7225805737622,-18.2258896078036,
16.5356516434534));
#167690=CARTESIAN_POINT('Origin',(-18.734,-18.952,0.));
#167691=CARTESIAN_POINT('',(-20.7225805855593,-18.2258896401121,17.5536949999931));
#167692=CARTESIAN_POINT('',(-20.7225805737355,-18.2258896077305,17.3329786086887));
#167693=CARTESIAN_POINT('',(-20.7225805737622,-18.2258896078036,0.));
#167694=CARTESIAN_POINT('',(-20.850999020182,-18.9502127631604,17.5117109399533));
#167695=CARTESIAN_POINT('Ctrl Pts',(-20.7225805855593,-18.2258896401121,
17.553694999993));
#167696=CARTESIAN_POINT('Ctrl Pts',(-20.7266285790002,-18.2369757801973,
17.552950415919));
#167697=CARTESIAN_POINT('Ctrl Pts',(-20.7305846696713,-18.2480979710921,
17.5522097264263));
#167698=CARTESIAN_POINT('Ctrl Pts',(-20.7395043458259,-18.2738554344083,
17.5505098677726));
#167699=CARTESIAN_POINT('Ctrl Pts',(-20.7444005421372,-18.2885111719396,
17.5495541086848));
#167700=CARTESIAN_POINT('Ctrl Pts',(-20.750899367023,-18.3086967657258,
17.5482546361465));
#167701=CARTESIAN_POINT('Ctrl Pts',(-20.7526404209504,-18.3141810910543,
17.5479032786566));
#167702=CARTESIAN_POINT('Ctrl Pts',(-20.7553758462965,-18.3229210900391,
17.5473461274144));
#167703=CARTESIAN_POINT('Ctrl Pts',(-20.7563847482496,-18.3261721343886,
17.5471394933976));
#167704=CARTESIAN_POINT('Ctrl Pts',(-20.7584558538732,-18.33290329118,17.5467129504672));
#167705=CARTESIAN_POINT('Ctrl Pts',(-20.7595169279054,-18.3363837119768,
17.5464931136084));
#167706=CARTESIAN_POINT('Ctrl Pts',(-20.7620296890385,-18.3447026276586,
17.5459693240063));
#167707=CARTESIAN_POINT('Ctrl Pts',(-20.7634730525617,-18.3495436545245,
17.5456658569024));
#167708=CARTESIAN_POINT('Ctrl Pts',(-20.7683087921699,-18.365977276532,
17.544640090409));
#167709=CARTESIAN_POINT('Ctrl Pts',(-20.7716193511503,-18.3775939681374,
17.5439224008817));
#167710=CARTESIAN_POINT('Ctrl Pts',(-20.7793503161945,-18.405629988541,
17.5422066981606));
#167711=CARTESIAN_POINT('Ctrl Pts',(-20.7836727516699,-18.422075709297,
17.5412137329758));
#167712=CARTESIAN_POINT('Ctrl Pts',(-20.7992282069319,-18.4843001268574,
17.537501174438));
#167713=CARTESIAN_POINT('Ctrl Pts',(-20.8091300683324,-18.5304000817769,
17.5348408066407));
#167714=CARTESIAN_POINT('Ctrl Pts',(-20.839677969429,-18.700030258527,17.5252552166219));
#167715=CARTESIAN_POINT('Ctrl Pts',(-20.8508934167311,-18.824991233221,
17.5185706624773));
#167716=CARTESIAN_POINT('Ctrl Pts',(-20.850999243967,-18.9502108540428,
17.5117114353352));
#167717=CARTESIAN_POINT('Ctrl Pts',(-20.8509992455974,-18.9502127843178,
17.5117113295994));
#167718=CARTESIAN_POINT('Ctrl Pts',(-20.8510695262169,-19.0334618402732,
17.5071511472245));
#167719=CARTESIAN_POINT('Ctrl Pts',(-20.8462293176907,-19.1166379126245,
17.5025270519463));
#167720=CARTESIAN_POINT('Ctrl Pts',(-20.8325132046076,-19.2332451195831,
17.4958024131623));
#167721=CARTESIAN_POINT('Ctrl Pts',(-20.8277008026706,-19.2670765721156,
17.4938228650143));
#167722=CARTESIAN_POINT('Ctrl Pts',(-20.8203841631101,-19.310880315912,
17.4912165050731));
#167723=CARTESIAN_POINT('Ctrl Pts',(-20.8186230170447,-19.3209726663742,
17.4906130039197));
#167724=CARTESIAN_POINT('Ctrl Pts',(-20.8155218560417,-19.3380127245543,
17.4895887993749));
#167725=CARTESIAN_POINT('Ctrl Pts',(-20.8142201261234,-19.3449672832719,
17.4891693092348));
#167726=CARTESIAN_POINT('Ctrl Pts',(-20.8115753898661,-19.3587154474302,
17.4883370439448));
#167727=CARTESIAN_POINT('Ctrl Pts',(-20.8102338631363,-19.3655092496791,
17.4879243205081));
#167728=CARTESIAN_POINT('Ctrl Pts',(-20.8075792012131,-19.3786144078015,
17.4871253293806));
#167729=CARTESIAN_POINT('Ctrl Pts',(-20.8062705223735,-19.3849265957684,
17.4867392082836));
#167730=CARTESIAN_POINT('Ctrl Pts',(-20.8031922253141,-19.3994404235502,
17.4858483918317));
#167731=CARTESIAN_POINT('Ctrl Pts',(-20.8014026463276,-19.4076376770188,
17.4853430613936));
#167732=CARTESIAN_POINT('Ctrl Pts',(-20.7964820731091,-19.4295506466621,
17.483986196528));
#167733=CARTESIAN_POINT('Ctrl Pts',(-20.7932630478049,-19.4432459740009,
17.4831318485563));
#167734=CARTESIAN_POINT('Ctrl Pts',(-20.7649958663005,-19.5583456074873,
17.4758971160508));
#167735=CARTESIAN_POINT('Ctrl Pts',(-20.7326147078825,-19.6577852284586,
17.4692780254053));
#167736=CARTESIAN_POINT('Ctrl Pts',(-20.6610715696034,-19.8324515836869,
17.4570100463674));
#167737=CARTESIAN_POINT('Ctrl Pts',(-20.6244765246981,-19.9085025570576,
17.451433154835));
#167738=CARTESIAN_POINT('Ctrl Pts',(-20.5381977865182,-20.063398031067,
17.4397198098766));
#167739=CARTESIAN_POINT('Ctrl Pts',(-20.4876434191509,-20.1415682249568,
17.4335968453404));
#167740=CARTESIAN_POINT('Ctrl Pts',(-20.4137245280448,-20.2408608798846,
17.4257440962747));
#167741=CARTESIAN_POINT('Ctrl Pts',(-20.3948022331264,-20.2651538488293,
17.4238168235806));
#167742=CARTESIAN_POINT('Ctrl Pts',(-20.3708599262467,-20.2945458102632,
17.4214862789034));
#167743=CARTESIAN_POINT('Ctrl Pts',(-20.3663363358639,-20.3000421954618,
17.421050517244));
#167744=CARTESIAN_POINT('Ctrl Pts',(-20.3591745750054,-20.3086551777334,
17.4203679008892));
#167745=CARTESIAN_POINT('Ctrl Pts',(-20.356555013109,-20.3117870791417,
17.4201197331622));
#167746=CARTESIAN_POINT('Ctrl Pts',(-20.351624142597,-20.317647802847,17.4196554619898));
#167747=CARTESIAN_POINT('Ctrl Pts',(-20.3493150076173,-20.3203783155646,
17.4194392130833));
#167748=CARTESIAN_POINT('Ctrl Pts',(-20.3440048979135,-20.3266252576383,
17.4189445809203));
#167749=CARTESIAN_POINT('Ctrl Pts',(-20.3409993215095,-20.3301377114932,
17.4186665407722));
#167750=CARTESIAN_POINT('Ctrl Pts',(-20.3330828580916,-20.3393281399851,
17.4179391539201));
#167751=CARTESIAN_POINT('Ctrl Pts',(-20.3281531834687,-20.3449899448515,
17.4174911574037));
#167752=CARTESIAN_POINT('Ctrl Pts',(-20.2945560036734,-20.3831648649959,
17.4144703435428));
#167753=CARTESIAN_POINT('Ctrl Pts',(-20.2649237166947,-20.4148195594296,
17.4119645343398));
#167754=CARTESIAN_POINT('Ctrl Pts',(-20.1835998145477,-20.4965133857353,
17.4054236572952));
#167755=CARTESIAN_POINT('Ctrl Pts',(-20.1302937814578,-20.5448672994004,
17.4014724000781));
#167756=CARTESIAN_POINT('Ctrl Pts',(-20.0058451160796,-20.6466968397585,
17.392707799697));
#167757=CARTESIAN_POINT('Ctrl Pts',(-19.933588696755,-20.6985892974522,
17.3879174280155));
#167758=CARTESIAN_POINT('Ctrl Pts',(-19.7972997306427,-20.7840106376653,
17.3790773092358));
#167759=CARTESIAN_POINT('Ctrl Pts',(-19.7344089441507,-20.8190966793269,
17.3750666298382));
#167760=CARTESIAN_POINT('Ctrl Pts',(-19.6453082205645,-20.8630089863234,
17.3693856194332));
#167761=CARTESIAN_POINT('Ctrl Pts',(-19.6205279724454,-20.8746299896293,
17.3678060415376));
#167762=CARTESIAN_POINT('Ctrl Pts',(-19.5772513509196,-20.8939105519997,
17.3650437045443));
#167763=CARTESIAN_POINT('Ctrl Pts',(-19.5588584719605,-20.9017943208189,
17.3638685595109));
#167764=CARTESIAN_POINT('Ctrl Pts',(-19.5322720645011,-20.9127465850986,
17.3621671675772));
#167765=CARTESIAN_POINT('Ctrl Pts',(-19.5241666156303,-20.9160270303605,
17.3616480997127));
#167766=CARTESIAN_POINT('Ctrl Pts',(-19.5099910500453,-20.9216622245086,
17.3607395802514));
#167767=CARTESIAN_POINT('Ctrl Pts',(-19.5039299225899,-20.9240393761907,
17.360350889664));
#167768=CARTESIAN_POINT('Ctrl Pts',(-19.4922774704833,-20.9285475155234,
17.3596031568151));
#167769=CARTESIAN_POINT('Ctrl Pts',(-19.4866878799951,-20.9306828339909,
17.3592442645864));
#167770=CARTESIAN_POINT('Ctrl Pts',(-19.4720715059446,-20.9361956410871,
17.3583052008593));
#167771=CARTESIAN_POINT('Ctrl Pts',(-19.4630306532431,-20.9395352051783,
17.3577237672871));
#167772=CARTESIAN_POINT('Ctrl Pts',(-19.4318254212238,-20.9508204198185,
17.3557147217561));
#167773=CARTESIAN_POINT('Ctrl Pts',(-19.4095521047387,-20.958457742573,
17.3542769330927));
#167774=CARTESIAN_POINT('Ctrl Pts',(-19.227864233617,-21.0173887515002,
17.3425137850433));
#167775=CARTESIAN_POINT('Ctrl Pts',(-19.0630323608603,-21.0499632506091,
17.331555211189));
#167776=CARTESIAN_POINT('Ctrl Pts',(-18.7712099510454,-21.0723772608182,
17.312213430873));
#167777=CARTESIAN_POINT('Ctrl Pts',(-18.6456783000796,-21.0708653071399,
17.3039353141196));
#167778=CARTESIAN_POINT('Ctrl Pts',(-18.5090983611205,-21.057053803406,
17.2954216778607));
#167779=CARTESIAN_POINT('Ctrl Pts',(-18.4971999757858,-21.0557485653287,
17.2946842650551));
#167780=CARTESIAN_POINT('Ctrl Pts',(-18.4803148521982,-21.053751216658,
17.2936444721052));
#167781=CARTESIAN_POINT('Ctrl Pts',(-18.4753187790598,-21.0531421556078,
17.2933376438129));
#167782=CARTESIAN_POINT('Ctrl Pts',(-18.4667179063014,-21.0520624984887,
17.2928109200508));
#167783=CARTESIAN_POINT('Ctrl Pts',(-18.4631120750835,-21.0516004258151,
17.292590548237));
#167784=CARTESIAN_POINT('Ctrl Pts',(-18.4561272117378,-21.050687050161,
17.2921645614603));
#167785=CARTESIAN_POINT('Ctrl Pts',(-18.4527480794268,-21.0502368737881,
17.2919588817362));
#167786=CARTESIAN_POINT('Ctrl Pts',(-18.4436430440941,-21.0490014878938,
17.2914057333722));
#167787=CARTESIAN_POINT('Ctrl Pts',(-18.4379191961337,-21.0482009830732,
17.2910591223061));
#167788=CARTESIAN_POINT('Ctrl Pts',(-18.416739362049,-21.0451504088812,
17.2897804897764));
#167789=CARTESIAN_POINT('Ctrl Pts',(-18.4013047068568,-21.0427526923624,
17.2888564416926));
#167790=CARTESIAN_POINT('Ctrl Pts',(-18.2517875119768,-21.0178280199976,
17.2799681064258));
#167791=CARTESIAN_POINT('Ctrl Pts',(-18.120123620421,-20.9826009742182,
17.2726210040869));
#167792=CARTESIAN_POINT('Ctrl Pts',(-17.8473499671938,-20.8806345077521,
17.2568069650021));
#167793=CARTESIAN_POINT('Ctrl Pts',(-17.708401958035,-20.8104726312299,
17.2483533301633));
#167794=CARTESIAN_POINT('Ctrl Pts',(-17.5605536548037,-20.7141478848008,
17.2380769063227));
#167795=CARTESIAN_POINT('Ctrl Pts',(-17.5429072246168,-20.7022683922302,
17.2368286278881));
#167796=CARTESIAN_POINT('Ctrl Pts',(-17.5180625448446,-20.684993340224,
17.2350385655076));
#167797=CARTESIAN_POINT('Ctrl Pts',(-17.510714681298,-20.6798144684435,
17.234505019022));
#167798=CARTESIAN_POINT('Ctrl Pts',(-17.4980925964965,-20.6707973807744,
17.2335812327407));
#167799=CARTESIAN_POINT('Ctrl Pts',(-17.4928026809292,-20.6669812709924,
17.2331918471486));
#167800=CARTESIAN_POINT('Ctrl Pts',(-17.4827058285511,-20.6596262840938,
17.2324443095098));
#167801=CARTESIAN_POINT('Ctrl Pts',(-17.4778960507041,-20.656091399268,
17.2320863148529));
#167802=CARTESIAN_POINT('Ctrl Pts',(-17.4654233759976,-20.6468432700202,
17.2311529854179));
#167803=CARTESIAN_POINT('Ctrl Pts',(-17.457784171652,-20.6410984327993,
17.2305764185805));
#167804=CARTESIAN_POINT('Ctrl Pts',(-17.4318444734706,-20.6213148223869,
17.2286015560826));
#167805=CARTESIAN_POINT('Ctrl Pts',(-17.4137351301006,-20.6070291836654,
17.2271935429105));
#167806=CARTESIAN_POINT('Ctrl Pts',(-17.2606449930511,-20.4821516166951,
17.215032336043));
#167807=CARTESIAN_POINT('Ctrl Pts',(-17.1396071314855,-20.3555765989584,
17.2035843977549));
#167808=CARTESIAN_POINT('Ctrl Pts',(-16.9831369067,-20.1452560628161,17.1862637157592));
#167809=CARTESIAN_POINT('Ctrl Pts',(-16.9352051229845,-20.0716966232254,
17.1804815539708));
#167810=CARTESIAN_POINT('Ctrl Pts',(-16.8732450303252,-19.9623087769314,
17.1724538775296));
#167811=CARTESIAN_POINT('Ctrl Pts',(-16.8554095330915,-19.928745184233,
17.170063395062));
#167812=CARTESIAN_POINT('Ctrl Pts',(-16.8351098744618,-19.8879288294555,
17.1672581905981));
#167813=CARTESIAN_POINT('Ctrl Pts',(-16.8317701006238,-19.8811221106966,
17.1667937182804));
#167814=CARTESIAN_POINT('Ctrl Pts',(-16.8266439153093,-19.8705310422349,
17.1660763468545));
#167815=CARTESIAN_POINT('Ctrl Pts',(-16.8248320740249,-19.8667591707565,
17.1658219086481));
#167816=CARTESIAN_POINT('Ctrl Pts',(-16.8214979542809,-19.8597651810801,
17.1653520823024));
#167817=CARTESIAN_POINT('Ctrl Pts',(-16.8199726409069,-19.8565446190239,
17.1651365112287));
#167818=CARTESIAN_POINT('Ctrl Pts',(-16.8165492740957,-19.8492690557924,
17.1646512443249));
#167819=CARTESIAN_POINT('Ctrl Pts',(-16.814655953314,-19.8452118875449,
17.1643818425557));
#167820=CARTESIAN_POINT('Ctrl Pts',(-16.8091248003533,-19.833260470886,
17.1635916999788));
#167821=CARTESIAN_POINT('Ctrl Pts',(-16.8055226483594,-19.8253496790139,
17.1630731070649));
#167822=CARTESIAN_POINT('Ctrl Pts',(-16.7804085174573,-19.7692827357452,
17.1594271870966));
#167823=CARTESIAN_POINT('Ctrl Pts',(-16.7606521474861,-19.7203553816621,
17.156398941036));
#167824=CARTESIAN_POINT('Ctrl Pts',(-16.7373630223412,-19.6558329690251,
17.1525392329145));
#167825=CARTESIAN_POINT('Ctrl Pts',(-16.7321508787293,-19.6408687700225,
17.1516532436768));
#167826=CARTESIAN_POINT('Ctrl Pts',(-16.7109435884538,-19.5777079244072,
17.147946742212));
#167827=CARTESIAN_POINT('Ctrl Pts',(-16.6965167799816,-19.5290009753863,
17.145168636274));
#167828=CARTESIAN_POINT('Ctrl Pts',(-16.6565769513346,-19.373867983843,
17.1364468229742));
#167829=CARTESIAN_POINT('Ctrl Pts',(-16.6375537615508,-19.265960843546,
17.1305558812288));
#167830=CARTESIAN_POINT('Ctrl Pts',(-16.6216106654859,-19.1021504885194,
17.1214049149708));
#167831=CARTESIAN_POINT('Ctrl Pts',(-16.6184150535142,-19.0470450235747,
17.1182935978638));
#167832=CARTESIAN_POINT('Ctrl Pts',(-16.6167287782852,-18.9575470175329,
17.1131438566884));
#167833=CARTESIAN_POINT('Ctrl Pts',(-16.6169173792691,-18.9232045909833,
17.1111449354558));
#167834=CARTESIAN_POINT('Ctrl Pts',(-16.6182634646052,-18.8780755499623,
17.1084822194833));
#167835=CARTESIAN_POINT('Ctrl Pts',(-16.6186686240855,-18.8672705775777,
17.107841999799));
#167836=CARTESIAN_POINT('Ctrl Pts',(-16.6194678522679,-18.8495773849862,
17.1067890314628));
#167837=CARTESIAN_POINT('Ctrl Pts',(-16.6198128568608,-18.8426870642994,
17.1063778255992));
#167838=CARTESIAN_POINT('Ctrl Pts',(-16.6205459278243,-18.829351839316,
17.1055797304374));
#167839=CARTESIAN_POINT('Ctrl Pts',(-16.6209298108531,-18.8229067746896,
17.1051929768543));
#167840=CARTESIAN_POINT('Ctrl Pts',(-16.6218843373953,-18.8080282081486,
17.1042977371976));
#167841=CARTESIAN_POINT('Ctrl Pts',(-16.6224760171326,-18.7995962086847,
17.1037885956355));
#167842=CARTESIAN_POINT('Ctrl Pts',(-16.6242032878061,-18.7769261807373,
17.1024148165201));
#167843=CARTESIAN_POINT('Ctrl Pts',(-16.6254324868048,-18.762695917692,
17.1015472544075));
#167844=CARTESIAN_POINT('Ctrl Pts',(-16.6403656975414,-18.6080816605446,
17.0920626676959));
#167845=CARTESIAN_POINT('Ctrl Pts',(-16.6679204806769,-18.4694168577996,
17.0829959915786));
#167846=CARTESIAN_POINT('Ctrl Pts',(-16.7372284608753,-18.242120645508,
17.0673628311088));
#167847=CARTESIAN_POINT('Ctrl Pts',(-16.7717048783854,-18.1517354615935,
17.0609354431817));
#167848=CARTESIAN_POINT('Ctrl Pts',(-16.8327736612588,-18.0195703079126,
17.0514347346944));
#167849=CARTESIAN_POINT('Ctrl Pts',(-16.8548502235409,-17.9758424958889,
17.0482747682353));
#167850=CARTESIAN_POINT('Ctrl Pts',(-16.8910617351461,-17.9099075468264,
17.0435245514821));
#167851=CARTESIAN_POINT('Ctrl Pts',(-16.904126168122,-17.8871337947401,
17.0418866803956));
#167852=CARTESIAN_POINT('Ctrl Pts',(-16.9210832996784,-17.8588084691842,
17.0398587510873));
#167853=CARTESIAN_POINT('Ctrl Pts',(-16.9245829012481,-17.8530257278042,
17.039445232032));
#167854=CARTESIAN_POINT('Ctrl Pts',(-16.9301992783735,-17.8438447838953,
17.0387896199361));
#167855=CARTESIAN_POINT('Ctrl Pts',(-16.9322980664955,-17.8404357104777,
17.0385463786577));
#167856=CARTESIAN_POINT('Ctrl Pts',(-16.9362988798129,-17.8339782684281,
17.0380860458462));
#167857=CARTESIAN_POINT('Ctrl Pts',(-16.9381989711154,-17.830928827148,
17.0378688393651));
#167858=CARTESIAN_POINT('Ctrl Pts',(-16.9425929354552,-17.8239168250786,
17.0373697765376));
#167859=CARTESIAN_POINT('Ctrl Pts',(-16.9450921957221,-17.8199576910739,
17.0370882800091));
#167860=CARTESIAN_POINT('Ctrl Pts',(-16.951830798566,-17.8093609643162,
17.0363355230918));
#167861=CARTESIAN_POINT('Ctrl Pts',(-16.9560941277454,-17.8027386101618,
17.0358658072725));
#167862=CARTESIAN_POINT('Ctrl Pts',(-16.9884370261509,-17.7531101513779,
17.0323498909384));
#167863=CARTESIAN_POINT('Ctrl Pts',(-17.0180388274937,-17.7111111495177,
17.0293980441262));
#167864=CARTESIAN_POINT('Ctrl Pts',(-17.0626704741397,-17.6524439651622,
17.0252455293426));
#167865=CARTESIAN_POINT('Ctrl Pts',(-17.076480291065,-17.6348755810427,
17.0239980918122));
#167866=CARTESIAN_POINT('Ctrl Pts',(-17.1195097664553,-17.5818837300231,
17.0202124901868));
#167867=CARTESIAN_POINT('Ctrl Pts',(-17.149606423822,-17.5471887870443,
17.0177016909427));
#167868=CARTESIAN_POINT('Ctrl Pts',(-17.2551132129274,-17.4332700014714,
17.0092480620041));
#167869=CARTESIAN_POINT('Ctrl Pts',(-17.335522033852,-17.3589195148344,
17.0033598456689));
#167870=CARTESIAN_POINT('Ctrl Pts',(-17.4645496538013,-17.2569418063313,
16.9942152161125));
#167871=CARTESIAN_POINT('Ctrl Pts',(-17.5091038410045,-17.2244713560694,
16.9911075315518));
#167872=CARTESIAN_POINT('Ctrl Pts',(-17.5833664007015,-17.1746681709009,
16.9859632669315));
#167873=CARTESIAN_POINT('Ctrl Pts',(-17.6123199771704,-17.1562550737006,
16.9839660796235));
#167874=CARTESIAN_POINT('Ctrl Pts',(-17.6509662038036,-17.1329772864511,
16.9813053462602));
#167875=CARTESIAN_POINT('Ctrl Pts',(-17.6602678219077,-17.1274712829664,
16.9806653304793));
#167876=CARTESIAN_POINT('Ctrl Pts',(-17.675573974019,-17.1185685360993,
16.9796126121064));
#167877=CARTESIAN_POINT('Ctrl Pts',(-17.6815537401217,-17.1151294401533,
16.9792014508654));
#167878=CARTESIAN_POINT('Ctrl Pts',(-17.6931629814044,-17.1085280063909,
16.97840338128));
#167879=CARTESIAN_POINT('Ctrl Pts',(-17.6987903321349,-17.1053620732191,
16.9780166083275));
#167880=CARTESIAN_POINT('Ctrl Pts',(-17.7118194671034,-17.0981101869123,
16.977121234935));
#167881=CARTESIAN_POINT('Ctrl Pts',(-17.7192313839569,-17.0940427524946,
16.9766119783896));
#167882=CARTESIAN_POINT('Ctrl Pts',(-17.739235676222,-17.0832204156952,
16.9752376878263));
#167883=CARTESIAN_POINT('Ctrl Pts',(-17.7518722409626,-17.0765485226784,
16.9743697258596));
#167884=CARTESIAN_POINT('Ctrl Pts',(-17.8684340106715,-17.016506977069,
16.9663637394059));
#167885=CARTESIAN_POINT('Ctrl Pts',(-17.976525859467,-16.97170637349,16.9589240495139));
#167886=CARTESIAN_POINT('Ctrl Pts',(-18.2426368976508,-16.8863988150121,
16.9406706497531));
#167887=CARTESIAN_POINT('Ctrl Pts',(-18.4027307136964,-16.8547621316976,
16.9297170534721));
#167888=CARTESIAN_POINT('Ctrl Pts',(-18.5973513535805,-16.8391634787584,
16.917309831331));
#167889=CARTESIAN_POINT('Ctrl Pts',(-18.6298937159241,-16.8373101480052,
16.915267206154));
#167890=CARTESIAN_POINT('Ctrl Pts',(-18.6697088681062,-16.8359640498544,
16.9128174343481));
#167891=CARTESIAN_POINT('Ctrl Pts',(-18.6769511939428,-16.8357564107192,
16.9123738193341));
#167892=CARTESIAN_POINT('Ctrl Pts',(-18.6883043083638,-16.8354892385981,
16.9116816835412));
#167893=CARTESIAN_POINT('Ctrl Pts',(-18.6924143676602,-16.8354044941909,
16.9114317893946));
#167894=CARTESIAN_POINT('Ctrl Pts',(-18.7000958400244,-16.8352684948106,
16.9109660421379));
#167895=CARTESIAN_POINT('Ctrl Pts',(-18.7036670967368,-16.8352143064694,
16.9107500331173));
#167896=CARTESIAN_POINT('Ctrl Pts',(-18.7118177015949,-16.835111264717,
16.9102582224434));
#167897=CARTESIAN_POINT('Ctrl Pts',(-18.7163970728415,-16.8350682321364,
16.9099827493544));
#167898=CARTESIAN_POINT('Ctrl Pts',(-18.7304665956651,-16.8349816773258,
16.9091389011255));
#167899=CARTESIAN_POINT('Ctrl Pts',(-18.7399570796502,-16.8349871081469,
16.9085731941461));
#167900=CARTESIAN_POINT('Ctrl Pts',(-18.8248564970574,-16.8356066218915,
16.9035413315385));
#167901=CARTESIAN_POINT('Ctrl Pts',(-18.9001911933304,-16.8401858786632,
16.8992789492573));
#167902=CARTESIAN_POINT('Ctrl Pts',(-19.0179552061379,-16.8536871815412,
16.892716497893));
#167903=CARTESIAN_POINT('Ctrl Pts',(-19.0606231991676,-16.859904227562,
16.8903599415697));
#167904=CARTESIAN_POINT('Ctrl Pts',(-19.2107231899026,-16.8864792634062,
16.88206090032));
#167905=CARTESIAN_POINT('Ctrl Pts',(-19.3167346056707,-16.9138487774787,
16.8761740322291));
#167906=CARTESIAN_POINT('Ctrl Pts',(-19.472260511082,-16.9671337025608,
16.8670325370955));
#167907=CARTESIAN_POINT('Ctrl Pts',(-19.5236473528516,-16.9870116502655,
16.8639266491064));
#167908=CARTESIAN_POINT('Ctrl Pts',(-19.6056756524519,-17.0224802057107,
16.8587850933084));
#167909=CARTESIAN_POINT('Ctrl Pts',(-19.6368163005452,-17.0368531098807,
16.8567887638693));
#167910=CARTESIAN_POINT('Ctrl Pts',(-19.6772925704882,-17.0567414621613,
16.8541290114569));
#167911=CARTESIAN_POINT('Ctrl Pts',(-19.6869554753732,-17.0615816192734,
16.8534890966186));
#167912=CARTESIAN_POINT('Ctrl Pts',(-19.7027243104024,-17.0696318663711,
16.8524365019883));
#167913=CARTESIAN_POINT('Ctrl Pts',(-19.7088524357667,-17.072798226157,
16.852025362836));
#167914=CARTESIAN_POINT('Ctrl Pts',(-19.7206868460627,-17.0789864495197,
16.8512273058944));
#167915=CARTESIAN_POINT('Ctrl Pts',(-19.7263950018332,-17.0820045851982,
16.8508405233371));
#167916=CARTESIAN_POINT('Ctrl Pts',(-19.7395460561159,-17.0890352591336,
16.8499450836638));
#167917=CARTESIAN_POINT('Ctrl Pts',(-19.7469788632167,-17.0930663497269,
16.8494357701368));
#167918=CARTESIAN_POINT('Ctrl Pts',(-19.7669102787446,-17.1040309410979,
16.848061226093));
#167919=CARTESIAN_POINT('Ctrl Pts',(-19.7793629816096,-17.1110465764857,
16.8471930659468));
#167920=CARTESIAN_POINT('Ctrl Pts',(-19.8931562728313,-17.1766825769026,
16.8391718406982));
#167921=CARTESIAN_POINT('Ctrl Pts',(-19.9895254231834,-17.2434792130333,
16.8317157764982));
#167922=CARTESIAN_POINT('Ctrl Pts',(-20.2060245923141,-17.4217896389405,
16.8133937656602));
#167923=CARTESIAN_POINT('Ctrl Pts',(-20.3197212627132,-17.5399488641614,
16.8023859059752));
#167924=CARTESIAN_POINT('Ctrl Pts',(-20.4378742552593,-17.6952164848327,
16.7899979178305));
#167925=CARTESIAN_POINT('Ctrl Pts',(-20.4564885302219,-17.7208518388757,
16.7880138528937));
#167926=CARTESIAN_POINT('Ctrl Pts',(-20.4786098198552,-17.7528014530596,
16.7856245165779));
#167927=CARTESIAN_POINT('Ctrl Pts',(-20.4826680678981,-17.7587269506774,
16.7851848234535));
#167928=CARTESIAN_POINT('Ctrl Pts',(-20.4889939386435,-17.7680650100906,
16.784497440466));
#167929=CARTESIAN_POINT('Ctrl Pts',(-20.4912818993623,-17.7714636338349,
16.7842484075076));
#167930=CARTESIAN_POINT('Ctrl Pts',(-20.4955471583454,-17.7778392866195,
16.78378340213));
#167931=CARTESIAN_POINT('Ctrl Pts',(-20.4975267620635,-17.7808146467676,
16.7835672789989));
#167932=CARTESIAN_POINT('Ctrl Pts',(-20.5020376687181,-17.7876319443204,
16.7830740862629));
#167933=CARTESIAN_POINT('Ctrl Pts',(-20.504563983472,-17.791477122827,16.7827973523673));
#167934=CARTESIAN_POINT('Ctrl Pts',(-20.5111393634606,-17.8015566317732,
16.78207562117));
#167935=CARTESIAN_POINT('Ctrl Pts',(-20.5151682022345,-17.8078041689976,
16.7816319402299));
#167936=CARTESIAN_POINT('Ctrl Pts',(-20.5417014523473,-17.8494291606566,
16.7786992181592));
#167937=CARTESIAN_POINT('Ctrl Pts',(-20.5631851567631,-17.8854498668355,
16.7762728279761));
#167938=CARTESIAN_POINT('Ctrl Pts',(-20.5941595696157,-17.9410758066855,
16.7726551234392));
#167939=CARTESIAN_POINT('Ctrl Pts',(-20.6044401401784,-17.9602262946154,
16.771432146629));
#167940=CARTESIAN_POINT('Ctrl Pts',(-20.6222691366742,-17.9947015518818,
16.7692644778012));
#167941=CARTESIAN_POINT('Ctrl Pts',(-20.6299303041583,-18.009965524945,
16.7683163897668));
#167942=CARTESIAN_POINT('Ctrl Pts',(-20.6692391383491,-18.0907061637996,
16.7633540808339));
#167943=CARTESIAN_POINT('Ctrl Pts',(-20.6976645159724,-18.1576525955934,
16.7594187150736));
#167944=CARTESIAN_POINT('Ctrl Pts',(-20.7225806455427,-18.225889804387,
16.7554729693871));
#167945=CARTESIAN_POINT('',(-20.8509999221897,-18.9514260237555,17.2909082342155));
#167946=CARTESIAN_POINT('Ctrl Pts',(-20.7225805737622,-18.2258896078036,
16.5356516434534));
#167947=CARTESIAN_POINT('Ctrl Pts',(-20.7222420301486,-18.2249624467816,
16.5357110395108));
#167948=CARTESIAN_POINT('Ctrl Pts',(-20.7219028372283,-18.2240355201043,
16.5357703973916));
#167949=CARTESIAN_POINT('Ctrl Pts',(-20.7191070459373,-18.2164118699226,
16.5362584073765));
#167950=CARTESIAN_POINT('Ctrl Pts',(-20.7166172251023,-18.2097272583708,
16.5366851133493));
#167951=CARTESIAN_POINT('Ctrl Pts',(-20.703129761205,-18.1740684980674,
16.5389556106031));
#167952=CARTESIAN_POINT('Ctrl Pts',(-20.6915300510584,-18.1453242498908,
16.5407655164785));
#167953=CARTESIAN_POINT('Ctrl Pts',(-20.6147736079762,-17.9665379995588,
16.5519561005528));
#167954=CARTESIAN_POINT('Ctrl Pts',(-20.5330352496231,-17.8242015957943,
16.560601236315));
#167955=CARTESIAN_POINT('Ctrl Pts',(-20.3657124080848,-17.5980980420755,
16.5759957468391));
#167956=CARTESIAN_POINT('Ctrl Pts',(-20.2879589757414,-17.5095222517557,
16.5825621627779));
#167957=CARTESIAN_POINT('Ctrl Pts',(-20.1929613260748,-17.4179448005569,
16.590292168564));
#167958=CARTESIAN_POINT('Ctrl Pts',(-20.1825655592422,-17.4081245802994,
16.5911342954128));
#167959=CARTESIAN_POINT('Ctrl Pts',(-20.1658644146375,-17.3926652596687,
16.5924816805941));
#167960=CARTESIAN_POINT('Ctrl Pts',(-20.1596232408126,-17.386957218988,
16.5929839921552));
#167961=CARTESIAN_POINT('Ctrl Pts',(-20.1485570617236,-17.3769574557105,
16.5938726153736));
#167962=CARTESIAN_POINT('Ctrl Pts',(-20.1437462839575,-17.3726500987316,
16.5942582599892));
#167963=CARTESIAN_POINT('Ctrl Pts',(-20.133756625154,-17.3637878107906,
16.5950577293174));
#167964=CARTESIAN_POINT('Ctrl Pts',(-20.1285750467172,-17.3592360485814,
16.5954716798637));
#167965=CARTESIAN_POINT('Ctrl Pts',(-20.1152202516283,-17.3476196440815,
16.5965367711511));
#167966=CARTESIAN_POINT('Ctrl Pts',(-20.1070151064927,-17.3405921619488,
16.5971894390735));
#167967=CARTESIAN_POINT('Ctrl Pts',(-20.0725673342631,-17.3115427079128,
16.5999227096948));
#167968=CARTESIAN_POINT('Ctrl Pts',(-20.0458470835339,-17.2900975812277,
16.6020265842632));
#167969=CARTESIAN_POINT('Ctrl Pts',(-19.9749016345451,-17.2359355160258,
16.6075743669528));
#167970=CARTESIAN_POINT('Ctrl Pts',(-19.9299029955634,-17.204278801301,
16.6110565452528));
#167971=CARTESIAN_POINT('Ctrl Pts',(-19.8068133545947,-17.1246656791153,
16.6204783095656));
#167972=CARTESIAN_POINT('Ctrl Pts',(-19.7267585893265,-17.0799670518381,
16.6265050649784));
#167973=CARTESIAN_POINT('Ctrl Pts',(-19.5956094518915,-17.0175236832881,
16.6361027564918));
#167974=CARTESIAN_POINT('Ctrl Pts',(-19.546291174055,-16.9963025073906,
16.6396526882863));
#167975=CARTESIAN_POINT('Ctrl Pts',(-19.4618465339254,-16.9637128297234,
16.645587671196));
#167976=CARTESIAN_POINT('Ctrl Pts',(-19.4271320951876,-16.951346467928,
16.6479878622863));
#167977=CARTESIAN_POINT('Ctrl Pts',(-19.3471239569802,-16.9251777609809,
16.6534058788003));
#167978=CARTESIAN_POINT('Ctrl Pts',(-19.3016518031468,-16.9119751084276,
16.6564037279012));
#167979=CARTESIAN_POINT('Ctrl Pts',(-19.2483051863362,-16.8984083830984,
16.6597975247556));
#167980=CARTESIAN_POINT('Ctrl Pts',(-19.240828275168,-16.8965503028953,
16.6602704030422));
#167981=CARTESIAN_POINT('Ctrl Pts',(-19.228840242613,-16.8936405593376,
16.6610239471918));
#167982=CARTESIAN_POINT('Ctrl Pts',(-19.2243356045278,-16.8925628320957,
16.6613060537998));
#167983=CARTESIAN_POINT('Ctrl Pts',(-19.2163369550479,-16.8906769000415,
16.6618050762793));
#167984=CARTESIAN_POINT('Ctrl Pts',(-19.2128443851018,-16.8898627794906,
16.6620223290233));
#167985=CARTESIAN_POINT('Ctrl Pts',(-19.2054214227456,-16.8881523571832,
16.6624826911082));
#167986=CARTESIAN_POINT('Ctrl Pts',(-19.2014905428926,-16.887258407569,
16.6627256648546));
#167987=CARTESIAN_POINT('Ctrl Pts',(-19.1908395447488,-16.8848681637446,
16.6633818753885));
#167988=CARTESIAN_POINT('Ctrl Pts',(-19.18411457444,-16.8833933986964,16.6637938945099));
#167989=CARTESIAN_POINT('Ctrl Pts',(-19.1502487982697,-16.8761397089737,
16.6658576989648));
#167990=CARTESIAN_POINT('Ctrl Pts',(-19.1230020420402,-16.8708617084941,
16.6674824896379));
#167991=CARTESIAN_POINT('Ctrl Pts',(-19.0432741923606,-16.857038180993,
16.6721539673701));
#167992=CARTESIAN_POINT('Ctrl Pts',(-18.9905631766393,-16.8499315761761,
16.6751387029452));
#167993=CARTESIAN_POINT('Ctrl Pts',(-18.7975121391367,-16.8312752159257,
16.685869490249));
#167994=CARTESIAN_POINT('Ctrl Pts',(-18.6563848057086,-16.8317439972712,
16.6933531304301));
#167995=CARTESIAN_POINT('Ctrl Pts',(-18.4249527490239,-16.855664962178,
16.7062229336917));
#167996=CARTESIAN_POINT('Ctrl Pts',(-18.334282573879,-16.8710497892409,
16.711414877912));
#167997=CARTESIAN_POINT('Ctrl Pts',(-18.231513257621,-16.8954530102101,
16.7176071698761));
#167998=CARTESIAN_POINT('Ctrl Pts',(-18.218153209067,-16.8987634032048,
16.7184181235569));
#167999=CARTESIAN_POINT('Ctrl Pts',(-18.1967888854907,-16.9042787959941,
16.71972489411));
#168000=CARTESIAN_POINT('Ctrl Pts',(-18.188763512746,-16.9064010459382,
16.7202180387283));
#168001=CARTESIAN_POINT('Ctrl Pts',(-18.1745418052073,-16.910251507313,
16.721096045105));
#168002=CARTESIAN_POINT('Ctrl Pts',(-18.1683404427557,-16.9119608721893,
16.7214802909954));
#168003=CARTESIAN_POINT('Ctrl Pts',(-18.155441417578,-16.9155797410592,
16.722282477645));
#168004=CARTESIAN_POINT('Ctrl Pts',(-18.1487452032223,-16.9174940832321,
16.7227005720818));
#168005=CARTESIAN_POINT('Ctrl Pts',(-18.131391715772,-16.9225479337874,
16.7237884479509));
#168006=CARTESIAN_POINT('Ctrl Pts',(-18.1207495961006,-16.9257383268636,
16.7244598845654));
#168007=CARTESIAN_POINT('Ctrl Pts',(-18.0747517122328,-16.9399235593037,
16.7273809648823));
#168008=CARTESIAN_POINT('Ctrl Pts',(-18.0396644231717,-16.9517605784893,
16.7296580666283));
#168009=CARTESIAN_POINT('Ctrl Pts',(-17.9473873520448,-16.9856116068852,
16.735781408014));
#168010=CARTESIAN_POINT('Ctrl Pts',(-17.8908153141529,-17.0091975774585,
16.7396765619259));
#168011=CARTESIAN_POINT('Ctrl Pts',(-17.6944560693447,-17.1012564693211,
16.7536824899201));
#168012=CARTESIAN_POINT('Ctrl Pts',(-17.5612889335845,-17.1826368251964,
16.7641254004742));
#168013=CARTESIAN_POINT('Ctrl Pts',(-17.4256691251995,-17.2876045165932,
16.775274728743));
#168014=CARTESIAN_POINT('Ctrl Pts',(-17.4132004202791,-17.297481794303,
16.7763045754062));
#168015=CARTESIAN_POINT('Ctrl Pts',(-17.3633098138706,-17.337926862869,
16.7804412366845));
#168016=CARTESIAN_POINT('Ctrl Pts',(-17.3268250501749,-17.3696336913954,
16.7835034127499));
#168017=CARTESIAN_POINT('Ctrl Pts',(-17.2857831522735,-17.4078442409456,
16.7869611033205));
#168018=CARTESIAN_POINT('Ctrl Pts',(-17.280140614872,-17.4131556483058,
16.7874367666734));
#168019=CARTESIAN_POINT('Ctrl Pts',(-17.2711626558328,-17.4217001995823,
16.7881938863815));
#168020=CARTESIAN_POINT('Ctrl Pts',(-17.2678085518274,-17.4249134887303,
16.7884768047266));
#168021=CARTESIAN_POINT('Ctrl Pts',(-17.2618823674125,-17.4306283988318,
16.7889767457891));
#168022=CARTESIAN_POINT('Ctrl Pts',(-17.2593060386514,-17.4331255502477,
16.7891941097726));
#168023=CARTESIAN_POINT('Ctrl Pts',(-17.2538539030307,-17.4384370770107,
16.7896541366006));
#168024=CARTESIAN_POINT('Ctrl Pts',(-17.2509797737923,-17.4412530987947,
16.7898966667735));
#168025=CARTESIAN_POINT('Ctrl Pts',(-17.2432338235334,-17.4488858520152,
16.7905504237056));
#168026=CARTESIAN_POINT('Ctrl Pts',(-17.238377277939,-17.4537181136533,
16.7909604483107));
#168027=CARTESIAN_POINT('Ctrl Pts',(-17.2142587984533,-17.4779501217995,
16.7929979049127));
#168028=CARTESIAN_POINT('Ctrl Pts',(-17.1953494862934,-17.4976990957821,
16.7945991609618));
#168029=CARTESIAN_POINT('Ctrl Pts',(-17.1416026067507,-17.55605480778,16.799181551355));
#168030=CARTESIAN_POINT('Ctrl Pts',(-17.1077966336604,-17.5955871643184,
16.8021035150069));
#168031=CARTESIAN_POINT('Ctrl Pts',(-16.9891049431107,-17.7452084395329,
16.8126800653688));
#168032=CARTESIAN_POINT('Ctrl Pts',(-16.9136618791501,-17.8623320950039,
16.8200706137296));
#168033=CARTESIAN_POINT('Ctrl Pts',(-16.8068179112161,-18.070686153413,
16.8330021879265));
#168034=CARTESIAN_POINT('Ctrl Pts',(-16.7691588994095,-18.1581857384207,
16.8383711955845));
#168035=CARTESIAN_POINT('Ctrl Pts',(-16.7329083146597,-18.260976911818,
16.8447602569049));
#168036=CARTESIAN_POINT('Ctrl Pts',(-16.7284301515187,-18.274083773018,
16.8455762488259));
#168037=CARTESIAN_POINT('Ctrl Pts',(-16.7214663083016,-18.2951389236566,
16.8468895906961));
#168038=CARTESIAN_POINT('Ctrl Pts',(-16.7188983072456,-18.3030597110123,
16.8473842248714));
#168039=CARTESIAN_POINT('Ctrl Pts',(-16.7144282204306,-18.3171297329511,
16.8482639473344));
#168040=CARTESIAN_POINT('Ctrl Pts',(-16.7125073147607,-18.3232729122047,
16.8486484114684));
#168041=CARTESIAN_POINT('Ctrl Pts',(-16.7085697250381,-18.3360701788467,
16.8494501118859));
#168042=CARTESIAN_POINT('Ctrl Pts',(-16.706557750201,-18.3427256239972,
16.8498674971716));
#168043=CARTESIAN_POINT('Ctrl Pts',(-16.7014310274273,-18.3599910105879,
16.8509514804946));
#168044=CARTESIAN_POINT('Ctrl Pts',(-16.6983665859002,-18.3706155592522,
16.8516197115848));
#168045=CARTESIAN_POINT('Ctrl Pts',(-16.6855348777617,-18.4164491517749,
16.8545078236665));
#168046=CARTESIAN_POINT('Ctrl Pts',(-16.6765972941571,-18.4518821008629,
16.8567544008797));
#168047=CARTESIAN_POINT('Ctrl Pts',(-16.6553861857809,-18.5462036424157,
16.8627748393013));
#168048=CARTESIAN_POINT('Ctrl Pts',(-16.644698373882,-18.605411281478,16.8665956013806));
#168049=CARTESIAN_POINT('Ctrl Pts',(-16.6139710412325,-18.8299646187728,
16.8812208442814));
#168050=CARTESIAN_POINT('Ctrl Pts',(-16.6109402702495,-18.9970091067736,
16.8924272711971));
#168051=CARTESIAN_POINT('Ctrl Pts',(-16.6329449335284,-19.2170295548752,
16.9067297600396));
#168052=CARTESIAN_POINT('Ctrl Pts',(-16.6404834758119,-19.2711594023646,
16.9102050133028));
#168053=CARTESIAN_POINT('Ctrl Pts',(-16.6516534379398,-19.3335739784397,
16.9141167542428));
#168054=CARTESIAN_POINT('Ctrl Pts',(-16.6532519873198,-19.342196898224,
16.9146550410336));
#168055=CARTESIAN_POINT('Ctrl Pts',(-16.6557506714089,-19.3552231673058,
16.9154647071087));
#168056=CARTESIAN_POINT('Ctrl Pts',(-16.65661129703,-19.3596338701279,16.9157382521202));
#168057=CARTESIAN_POINT('Ctrl Pts',(-16.6581797704984,-19.3675383031256,
16.916227339784));
#168058=CARTESIAN_POINT('Ctrl Pts',(-16.6588824007356,-19.3710330015503,
16.9164431742448));
#168059=CARTESIAN_POINT('Ctrl Pts',(-16.6604264787284,-19.3786137064543,
16.9169104885663));
#168060=CARTESIAN_POINT('Ctrl Pts',(-16.6612711751822,-19.3826989924671,
16.9171617803487));
#168061=CARTESIAN_POINT('Ctrl Pts',(-16.6636729891647,-19.3941443917744,
16.9178643375515));
#168062=CARTESIAN_POINT('Ctrl Pts',(-16.6652572889207,-19.4014988255602,
16.918314076231));
#168063=CARTESIAN_POINT('Ctrl Pts',(-16.6748611173275,-19.4449539748703,
16.9209622094855));
#168064=CARTESIAN_POINT('Ctrl Pts',(-16.6837867874714,-19.480850373623,
16.923111961268));
#168065=CARTESIAN_POINT('Ctrl Pts',(-16.7159760238316,-19.5971970646749,
16.9300102235489));
#168066=CARTESIAN_POINT('Ctrl Pts',(-16.7430730715202,-19.6765082426188,
16.9346045941927));
#168067=CARTESIAN_POINT('Ctrl Pts',(-16.8430743112417,-19.9207972901339,
16.9489788794502));
#168068=CARTESIAN_POINT('Ctrl Pts',(-16.9323569716125,-20.0781634485424,
16.9586444012629));
#168069=CARTESIAN_POINT('Ctrl Pts',(-17.0540570765474,-20.240406813255,
16.9704341212555));
#168070=CARTESIAN_POINT('Ctrl Pts',(-17.0679146180673,-20.2582770703781,
16.9717592439999));
#168071=CARTESIAN_POINT('Ctrl Pts',(-17.0879863379307,-20.2833218872036,
16.9736561843642));
#168072=CARTESIAN_POINT('Ctrl Pts',(-17.0939668880918,-20.2906823112529,
16.9742186695119));
#168073=CARTESIAN_POINT('Ctrl Pts',(-17.1037832329451,-20.3025990380786,
16.9751376373646));
#168074=CARTESIAN_POINT('Ctrl Pts',(-17.1075891965159,-20.3071798280818,
16.9754929075487));
#168075=CARTESIAN_POINT('Ctrl Pts',(-17.1156116581692,-20.31675304647,16.9762396554278));
#168076=CARTESIAN_POINT('Ctrl Pts',(-17.1198320382819,-20.3217421263506,
16.9766312899186));
#168077=CARTESIAN_POINT('Ctrl Pts',(-17.1299555941359,-20.3335978218622,
16.9775678963823));
#168078=CARTESIAN_POINT('Ctrl Pts',(-17.1358798241044,-20.340446216737,
16.9781137349578));
#168079=CARTESIAN_POINT('Ctrl Pts',(-17.1561244258381,-20.3635476986631,
16.9799715573836));
#168080=CARTESIAN_POINT('Ctrl Pts',(-17.1706498834008,-20.3796185034324,
16.9812920867932));
#168081=CARTESIAN_POINT('Ctrl Pts',(-17.2520210338456,-20.4669153775368,
16.9886245994275));
#168082=CARTESIAN_POINT('Ctrl Pts',(-17.3234792587851,-20.5336627178883,
16.994835812582));
#168083=CARTESIAN_POINT('Ctrl Pts',(-17.5099162840561,-20.6850965982024,
17.0104620336871));
#168084=CARTESIAN_POINT('Ctrl Pts',(-17.6293375144373,-20.7635526363035,
17.0200145367689));
#168085=CARTESIAN_POINT('Ctrl Pts',(-17.8089521712131,-20.8571448643554,
17.0331578346631));
#168086=CARTESIAN_POINT('Ctrl Pts',(-17.8633330561953,-20.882603771998,
17.0369878252698));
#168087=CARTESIAN_POINT('Ctrl Pts',(-17.927002448383,-20.9091725407835,
17.0412456547012));
#168088=CARTESIAN_POINT('Ctrl Pts',(-17.9352996383769,-20.9125731665961,
17.0417961938796));
#168089=CARTESIAN_POINT('Ctrl Pts',(-17.9478263141324,-20.917614537629,
17.0426205966818));
#168090=CARTESIAN_POINT('Ctrl Pts',(-17.9520397545371,-20.9192945255579,
17.0428967426908));
#168091=CARTESIAN_POINT('Ctrl Pts',(-17.9595769344767,-20.9222717185525,
17.0433886335362));
#168092=CARTESIAN_POINT('Ctrl Pts',(-17.9628985741172,-20.9235740718949,
17.0436046846649));
#168093=CARTESIAN_POINT('Ctrl Pts',(-17.9700824553348,-20.9263698060981,
17.0440703771532));
#168094=CARTESIAN_POINT('Ctrl Pts',(-17.973945778666,-20.9278602500142,
17.0443198416477));
#168095=CARTESIAN_POINT('Ctrl Pts',(-17.9847081014494,-20.9319760449427,
17.0450121501837));
#168096=CARTESIAN_POINT('Ctrl Pts',(-17.9916165733289,-20.9345766918909,
17.0454535384972));
#168097=CARTESIAN_POINT('Ctrl Pts',(-18.0310433374864,-20.9491836439789,
17.0479561804461));
#168098=CARTESIAN_POINT('Ctrl Pts',(-18.0638410686655,-20.9604267218073,
17.0499748109498));
#168099=CARTESIAN_POINT('Ctrl Pts',(-18.1686092808636,-20.9934887469145,
17.0562680637444));
#168100=CARTESIAN_POINT('Ctrl Pts',(-18.2414768688217,-21.0122829120892,
17.0604179200224));
#168101=CARTESIAN_POINT('Ctrl Pts',(-18.5047006749382,-21.0654062408314,
17.0750830272929));
#168102=CARTESIAN_POINT('Ctrl Pts',(-18.6985300441149,-21.0775118966688,
17.0853827311156));
#168103=CARTESIAN_POINT('Ctrl Pts',(-18.9124866154572,-21.0615692744244,
17.0978722171974));
#168104=CARTESIAN_POINT('Ctrl Pts',(-18.9336390197124,-21.0596726997015,
17.0991178779777));
#168105=CARTESIAN_POINT('Ctrl Pts',(-18.9630312679992,-21.0565909020386,
17.1008653210772));
#168106=CARTESIAN_POINT('Ctrl Pts',(-18.9712984965738,-21.0556747864598,
17.1013586523916));
#168107=CARTESIAN_POINT('Ctrl Pts',(-18.9855603310346,-21.0540092517808,
17.1022129342335));
#168108=CARTESIAN_POINT('Ctrl Pts',(-18.9915575636832,-21.053282845061,
17.1025731563047));
#168109=CARTESIAN_POINT('Ctrl Pts',(-19.0039713265761,-21.0517253022865,
17.1033208687463));
#168110=CARTESIAN_POINT('Ctrl Pts',(-19.0103873130794,-21.0508904006551,
17.1037084744519));
#168111=CARTESIAN_POINT('Ctrl Pts',(-19.0254065747516,-21.0488659087179,
17.1046185750984));
#168112=CARTESIAN_POINT('Ctrl Pts',(-19.0340065094453,-21.0476527674522,
17.1051418098431));
#168113=CARTESIAN_POINT('Ctrl Pts',(-19.0619171734273,-21.0435402544047,
17.1068469531146));
#168114=CARTESIAN_POINT('Ctrl Pts',(-19.081194870727,-21.0404266781636,
17.1080356146905));
#168115=CARTESIAN_POINT('Ctrl Pts',(-19.1796641441247,-21.0231216836101,
17.1141650097136));
#168116=CARTESIAN_POINT('Ctrl Pts',(-19.2580346514347,-21.0046925297819,
17.1192390786239));
#168117=CARTESIAN_POINT('Ctrl Pts',(-19.4872281638598,-20.9368147407889,
17.1346478897531));
#168118=CARTESIAN_POINT('Ctrl Pts',(-19.6337378918041,-20.8748382907497,
17.1452934873961));
#168119=CARTESIAN_POINT('Ctrl Pts',(-19.8277912654149,-20.7656745182451,
17.1597745925));
#168120=CARTESIAN_POINT('Ctrl Pts',(-19.8821872105743,-20.731736607114,
17.1638734363951));
#168121=CARTESIAN_POINT('Ctrl Pts',(-19.9425484966151,-20.6901554424236,
17.1683981386437));
#168122=CARTESIAN_POINT('Ctrl Pts',(-19.95009845222,-20.6848815228588,17.1689636296993));
#168123=CARTESIAN_POINT('Ctrl Pts',(-19.9613055878804,-20.6769436105449,
17.1698020666634));
#168124=CARTESIAN_POINT('Ctrl Pts',(-19.9649889174969,-20.6743169718378,
17.1700774680032));
#168125=CARTESIAN_POINT('Ctrl Pts',(-19.9714780795977,-20.6696579999997,
17.1705623379281));
#168126=CARTESIAN_POINT('Ctrl Pts',(-19.9742873622996,-20.6676305726915,
17.1707721379487));
#168127=CARTESIAN_POINT('Ctrl Pts',(-19.9771026961052,-20.6655882490026,
17.170982276612));
#168128=CARTESIAN_POINT('Ctrl Pts',(-19.9771136738019,-20.6655802853063,
17.170983095994));
#168129=CARTESIAN_POINT('Ctrl Pts',(-19.9771354433339,-20.6655644924265,
17.1709847208818));
#168130=CARTESIAN_POINT('Ctrl Pts',(-19.9771462357018,-20.6655566628618,
17.1709855264275));
#168131=CARTESIAN_POINT('Ctrl Pts',(-19.9771676399043,-20.6655411343959,
17.1709871240405));
#168132=CARTESIAN_POINT('Ctrl Pts',(-19.9771782513505,-20.6655334357815,
17.170987916079));
#168133=CARTESIAN_POINT('Ctrl Pts',(-19.9771992967715,-20.6655181670099,
17.1709894869063));
#168134=CARTESIAN_POINT('Ctrl Pts',(-19.9772097309217,-20.6655105967305,
17.1709902657083));
#168135=CARTESIAN_POINT('Ctrl Pts',(-19.977229852374,-20.6654959977512,
17.1709917675649));
#168136=CARTESIAN_POINT('Ctrl Pts',(-19.9772395398793,-20.665488968924,
17.1709924906349));
#168137=CARTESIAN_POINT('Ctrl Pts',(-19.9772588793793,-20.665474936784,
17.1709939341217));
#168138=CARTESIAN_POINT('Ctrl Pts',(-19.9772685307359,-20.6654679339352,
17.1709946544909));
#168139=CARTESIAN_POINT('Ctrl Pts',(-19.9772877963939,-20.6654539548757,
17.1709960924611));
#168140=CARTESIAN_POINT('Ctrl Pts',(-19.9772974112058,-20.6654469782955,
17.1709968101001));
#168141=CARTESIAN_POINT('Ctrl Pts',(-19.9773166058526,-20.6654330502682,
17.1709982427649));
#168142=CARTESIAN_POINT('Ctrl Pts',(-19.9773261851852,-20.6654260991863,
17.1709989577532));
#168143=CARTESIAN_POINT('Ctrl Pts',(-19.9773453071036,-20.6654122234426,
17.1710003849846));
#168144=CARTESIAN_POINT('Ctrl Pts',(-19.9773548504042,-20.6654052982629,
17.171001097281));
#168145=CARTESIAN_POINT('Ctrl Pts',(-19.9806584190717,-20.6630079925801,
17.1712476698269));
#168146=CARTESIAN_POINT('Ctrl Pts',(-19.9839455755235,-20.6606080953178,
17.1714928669859));
#168147=CARTESIAN_POINT('Ctrl Pts',(-19.9907411636819,-20.655616644728,
17.1719995009706));
#168148=CARTESIAN_POINT('Ctrl Pts',(-19.9942485519808,-20.6530236955077,
17.1722608409171));
#168149=CARTESIAN_POINT('Ctrl Pts',(-20.0031488824285,-20.6464012023043,
17.1729237095971));
#168150=CARTESIAN_POINT('Ctrl Pts',(-20.0085307082385,-20.6423567069021,
17.1733242436459));
#168151=CARTESIAN_POINT('Ctrl Pts',(-20.0240018453476,-20.63061409789,17.1744751195144));
#168152=CARTESIAN_POINT('Ctrl Pts',(-20.034041526479,-20.6228507104135,
17.175221290356));
#168153=CARTESIAN_POINT('Ctrl Pts',(-20.0682671456734,-20.5958897895153,
17.177765036077));
#168154=CARTESIAN_POINT('Ctrl Pts',(-20.0921035374571,-20.5762528834093,
17.1795366818744));
#168155=CARTESIAN_POINT('Ctrl Pts',(-20.2111558238006,-20.4737212301426,
17.1884346582502));
#168156=CARTESIAN_POINT('Ctrl Pts',(-20.2992558521049,-20.3829451181268,
17.195197038758));
#168157=CARTESIAN_POINT('Ctrl Pts',(-20.4088523546216,-20.247702555824,
17.2046738914946));
#168158=CARTESIAN_POINT('Ctrl Pts',(-20.437690006796,-20.2095435068449,
17.207288535583));
#168159=CARTESIAN_POINT('Ctrl Pts',(-20.5177923269409,-20.0957309612451,
17.2149889304014));
#168160=CARTESIAN_POINT('Ctrl Pts',(-20.5654773367654,-20.0177032377189,
17.2201527915231));
#168161=CARTESIAN_POINT('Ctrl Pts',(-20.6143678990597,-19.9246739637255,
17.2263139475871));
#168162=CARTESIAN_POINT('Ctrl Pts',(-20.6206458751859,-19.9124402135795,
17.2271241155909));
#168163=CARTESIAN_POINT('Ctrl Pts',(-20.6305202472311,-19.8927278016584,
17.228429861149));
#168164=CARTESIAN_POINT('Ctrl Pts',(-20.6341926876479,-19.8852875182859,
17.2289227732065));
#168165=CARTESIAN_POINT('Ctrl Pts',(-20.6406341832621,-19.8720415548439,
17.2298005119924));
#168166=CARTESIAN_POINT('Ctrl Pts',(-20.6434207110624,-19.8662444520911,
17.2301847241456));
#168167=CARTESIAN_POINT('Ctrl Pts',(-20.6491701054274,-19.8541424483194,
17.2309869883666));
#168168=CARTESIAN_POINT('Ctrl Pts',(-20.6521283521303,-19.8478354495841,
17.2314051948477));
#168169=CARTESIAN_POINT('Ctrl Pts',(-20.6597270499608,-19.8314247814691,
17.2324936855358));
#168170=CARTESIAN_POINT('Ctrl Pts',(-20.6643190860116,-19.8212990486623,
17.2331656284302));
#168171=CARTESIAN_POINT('Ctrl Pts',(-20.6838886323732,-19.7772272266871,
17.2360919506323));
#168172=CARTESIAN_POINT('Ctrl Pts',(-20.6980512870115,-19.7429285195912,
17.2383739101748));
#168173=CARTESIAN_POINT('Ctrl Pts',(-20.7332564627841,-19.6508837265034,
17.2445136879773));
#168174=CARTESIAN_POINT('Ctrl Pts',(-20.7526971487398,-19.5925666060741,
17.2484207466186));
#168175=CARTESIAN_POINT('Ctrl Pts',(-20.8236534047749,-19.3441763308729,
17.2651063524798));
#168176=CARTESIAN_POINT('Ctrl Pts',(-20.8510532927738,-19.1482730593989,
17.2784800810824));
#168177=CARTESIAN_POINT('Ctrl Pts',(-20.8509999221897,-18.9514260237555,
17.2909082342155));
#168178=CARTESIAN_POINT('Ctrl Pts',(-20.8509999215524,-18.9514236778724,
17.2909083823253));
#168179=CARTESIAN_POINT('Ctrl Pts',(-20.8509956361684,-18.935682207655,
17.2919022365754));
#168180=CARTESIAN_POINT('Ctrl Pts',(-20.8508157763398,-18.919940709559,
17.2928889660196));
#168181=CARTESIAN_POINT('Ctrl Pts',(-20.850214855114,-18.8933322838161,
17.2945432125346));
#168182=CARTESIAN_POINT('Ctrl Pts',(-20.8498856304743,-18.882464226158,
17.2952150250629));
#168183=CARTESIAN_POINT('Ctrl Pts',(-20.849291499802,-18.8668317566442,
17.2961753415949));
#168184=CARTESIAN_POINT('Ctrl Pts',(-20.8490942019215,-18.8620651524252,
17.2964673539702));
#168185=CARTESIAN_POINT('Ctrl Pts',(-20.8487208814448,-18.8537280704049,
17.2969766461215));
#168186=CARTESIAN_POINT('Ctrl Pts',(-20.8485519258228,-18.8501573174116,
17.2971943076044));
#168187=CARTESIAN_POINT('Ctrl Pts',(-20.8482044718159,-18.8431880863994,
17.2976181945417));
#168188=CARTESIAN_POINT('Ctrl Pts',(-20.848026821273,-18.8397895692581,
17.2978244667218));
#168189=CARTESIAN_POINT('Ctrl Pts',(-20.8476550554098,-18.8329920284264,
17.298236155742));
#168190=CARTESIAN_POINT('Ctrl Pts',(-20.8474609359881,-18.8295930435458,
17.2984415725897));
#168191=CARTESIAN_POINT('Ctrl Pts',(-20.846973681577,-18.8214082289121,
17.298935190113));
#168192=CARTESIAN_POINT('Ctrl Pts',(-20.8466724838614,-18.8166228724245,
17.2992229416761));
#168193=CARTESIAN_POINT('Ctrl Pts',(-20.8455076197931,-18.7990673600145,
17.3002756055668));
#168194=CARTESIAN_POINT('Ctrl Pts',(-20.8445443857378,-18.786303787924,
17.3010351496069));
#168195=CARTESIAN_POINT('Ctrl Pts',(-20.8412948271697,-18.7478907425378,
17.3033057236318));
#168196=CARTESIAN_POINT('Ctrl Pts',(-20.838656156522,-18.7222726321763,
17.3047993762694));
#168197=CARTESIAN_POINT('Ctrl Pts',(-20.8160114727723,-18.5358628444971,
17.3155583767712));
#168198=CARTESIAN_POINT('Ctrl Pts',(-20.7780845405037,-18.3778969488394,
17.3241155065484));
#168199=CARTESIAN_POINT('Ctrl Pts',(-20.7225805737356,-18.2258896077308,
17.3329786086887));
#168200=CARTESIAN_POINT('Origin',(-18.734,-18.952,0.));
#168201=CARTESIAN_POINT('',(-20.7225805841812,-18.2258896363379,18.3568546368673));
#168202=CARTESIAN_POINT('',(-20.7225805578635,-18.2258895642624,18.13180632455));
#168203=CARTESIAN_POINT('',(-20.7225805737622,-18.2258896078036,0.));
#168204=CARTESIAN_POINT('Ctrl Pts',(-20.7225805841812,-18.2258896363379,
18.3568546368673));
#168205=CARTESIAN_POINT('Ctrl Pts',(-20.727923816343,-18.2405230147683,
18.3558520868808));
#168206=CARTESIAN_POINT('Ctrl Pts',(-20.7331061395786,-18.2552170561466,
18.3548454415314));
#168207=CARTESIAN_POINT('Ctrl Pts',(-20.7819943705009,-18.3988736054763,
18.3450068227108));
#168208=CARTESIAN_POINT('Ctrl Pts',(-20.8133221923182,-18.5317079699484,
18.3359031584784));
#168209=CARTESIAN_POINT('Ctrl Pts',(-20.8417531210889,-18.7406859733689,
18.3221216814772));
#168210=CARTESIAN_POINT('Ctrl Pts',(-20.8479010506242,-18.8152459538833,
18.3173148853575));
#168211=CARTESIAN_POINT('Ctrl Pts',(-20.8503509139878,-18.8988371843921,
18.3121558368701));
#168212=CARTESIAN_POINT('Ctrl Pts',(-20.8505548518705,-18.9076937766778,
18.3116121302995));
#168213=CARTESIAN_POINT('Ctrl Pts',(-20.8507777609052,-18.9210041598406,
18.3107996272138));
#168214=CARTESIAN_POINT('Ctrl Pts',(-20.8508382797461,-18.9254570271004,
18.310528588847));
#168215=CARTESIAN_POINT('Ctrl Pts',(-20.8509183444085,-18.9331296582656,
18.3100629466643));
#168216=CARTESIAN_POINT('Ctrl Pts',(-20.8509445960285,-18.9363492967765,
18.3098679704955));
#168217=CARTESIAN_POINT('Ctrl Pts',(-20.8509874023568,-18.9436391203129,
18.3094274664756));
#168218=CARTESIAN_POINT('Ctrl Pts',(-20.8509995645971,-18.9477092909051,
18.3091821873668));
#168219=CARTESIAN_POINT('Ctrl Pts',(-20.8510007238652,-18.9588398526186,
18.3085132019213));
#168220=CARTESIAN_POINT('Ctrl Pts',(-20.8509661391233,-18.9659002674402,
18.3080907953781));
#168221=CARTESIAN_POINT('Ctrl Pts',(-20.8505991936105,-19.0029597814589,
18.3058832357657));
#168222=CARTESIAN_POINT('Ctrl Pts',(-20.8496644747793,-19.0329511230616,
18.3041297816601));
#168223=CARTESIAN_POINT('Ctrl Pts',(-20.8449576280264,-19.1226665407886,
18.298956837913));
#168224=CARTESIAN_POINT('Ctrl Pts',(-20.8392906833233,-19.1822636369617,
18.2956162480313));
#168225=CARTESIAN_POINT('Ctrl Pts',(-20.8082534011065,-19.4070597635603,
18.2831217660778));
#168226=CARTESIAN_POINT('Ctrl Pts',(-20.7658883757387,-19.5692821115655,
18.2742744347359));
#168227=CARTESIAN_POINT('Ctrl Pts',(-20.6832637936845,-19.779991040733,
18.2615099001174));
#168228=CARTESIAN_POINT('Ctrl Pts',(-20.6593332571522,-19.8342071298561,
18.2581085315601));
#168229=CARTESIAN_POINT('Ctrl Pts',(-20.6277538903282,-19.8983271407323,
18.2539095578999));
#168230=CARTESIAN_POINT('Ctrl Pts',(-20.6222502135285,-19.9092617072119,
18.2531871747713));
#168231=CARTESIAN_POINT('Ctrl Pts',(-20.6130255255541,-19.927199958927,
18.251991363438));
#168232=CARTESIAN_POINT('Ctrl Pts',(-20.609359395494,-19.9342316532726,
18.2515198662545));
#168233=CARTESIAN_POINT('Ctrl Pts',(-20.6026761213407,-19.9468764556063,
18.2506669537519));
#168234=CARTESIAN_POINT('Ctrl Pts',(-20.5996729629049,-19.9524968778072,
18.2502860377094));
#168235=CARTESIAN_POINT('Ctrl Pts',(-20.5931997995598,-19.9644809339232,
18.2494699188435));
#168236=CARTESIAN_POINT('Ctrl Pts',(-20.5897224046173,-19.9708404640606,
18.249034455803));
#168237=CARTESIAN_POINT('Ctrl Pts',(-20.5802117969951,-19.9880234293588,
18.2478513438037));
#168238=CARTESIAN_POINT('Ctrl Pts',(-20.5741161729741,-19.998811828969,
18.247101462982));
#168239=CARTESIAN_POINT('Ctrl Pts',(-20.5423240491179,-20.0539436306089,
18.2432324027919));
#168240=CARTESIAN_POINT('Ctrl Pts',(-20.5151199527809,-20.0973936585241,
18.2400588250411));
#168241=CARTESIAN_POINT('Ctrl Pts',(-20.3905655885019,-20.2811476841275,
18.2260769719922));
#168242=CARTESIAN_POINT('Ctrl Pts',(-20.2780252262199,-20.410359560337,
18.2147052045248));
#168243=CARTESIAN_POINT('Ctrl Pts',(-20.0828499636757,-20.5862471663019,
18.197426879911));
#168244=CARTESIAN_POINT('Ctrl Pts',(-20.0105246495634,-20.6433452711746,
18.1914506510582));
#168245=CARTESIAN_POINT('Ctrl Pts',(-19.9267413830612,-20.7010427300654,
18.1851657057317));
#168246=CARTESIAN_POINT('Ctrl Pts',(-19.9187408297852,-20.7064719014111,
18.184571666022));
#168247=CARTESIAN_POINT('Ctrl Pts',(-19.9068673208059,-20.714411001995,
18.1836993899339));
#168248=CARTESIAN_POINT('Ctrl Pts',(-19.9030230341607,-20.7169632967005,
18.18341840493));
#168249=CARTESIAN_POINT('Ctrl Pts',(-19.896185488613,-20.7214707320428,
18.1829212180328));
#168250=CARTESIAN_POINT('Ctrl Pts',(-19.8931955948251,-20.7234308778818,
18.1827046830001));
#168251=CARTESIAN_POINT('Ctrl Pts',(-19.8867759877724,-20.7276162975148,
18.1822416376643));
#168252=CARTESIAN_POINT('Ctrl Pts',(-19.8833447995145,-20.7298392071457,
18.1819952847579));
#168253=CARTESIAN_POINT('Ctrl Pts',(-19.8739015190362,-20.7359183113465,
18.1813203333773));
#168254=CARTESIAN_POINT('Ctrl Pts',(-19.8678762534227,-20.7397540826111,
18.1808930738412));
#168255=CARTESIAN_POINT('Ctrl Pts',(-19.8354946863946,-20.7601390921028,
18.1786143173532));
#168256=CARTESIAN_POINT('Ctrl Pts',(-19.8087937969521,-20.7761370687922,
18.1767969984881));
#168257=CARTESIAN_POINT('Ctrl Pts',(-19.6393308138361,-20.8726581660643,
18.1655817890799));
#168258=CARTESIAN_POINT('Ctrl Pts',(-19.4879600380041,-20.936970608127,
18.1569210803046));
#168259=CARTESIAN_POINT('Ctrl Pts',(-19.21821219991,-21.016210652848,18.1415316974819));
#168260=CARTESIAN_POINT('Ctrl Pts',(-19.1032203146341,-21.0398453333557,
18.1349896364419));
#168261=CARTESIAN_POINT('Ctrl Pts',(-18.9726798992676,-21.0555506288579,
18.1272870429984));
#168262=CARTESIAN_POINT('Ctrl Pts',(-18.9584707408627,-21.0571142995226,
18.1264452480962));
#168263=CARTESIAN_POINT('Ctrl Pts',(-18.9358327566271,-21.0593737316021,
18.1250982948451));
#168264=CARTESIAN_POINT('Ctrl Pts',(-18.9274135615199,-21.0601631097593,
18.1245960802784));
#168265=CARTESIAN_POINT('Ctrl Pts',(-18.9125575902411,-21.0614662549206,
18.1237075700652));
#168266=CARTESIAN_POINT('Ctrl Pts',(-18.906122733441,-21.0620010561345,
18.1233219409166));
#168267=CARTESIAN_POINT('Ctrl Pts',(-18.8928091429336,-21.0630462413223,
18.1225224461373));
#168268=CARTESIAN_POINT('Ctrl Pts',(-18.8859301677541,-21.0635524618761,
18.1221084543894));
#168269=CARTESIAN_POINT('Ctrl Pts',(-18.8682680002355,-21.064765457926,
18.121043135992));
#168270=CARTESIAN_POINT('Ctrl Pts',(-18.8574817455996,-21.0654232959384,
18.1203902809032));
#168271=CARTESIAN_POINT('Ctrl Pts',(-18.8124547121445,-21.0678235554727,
18.1176551976899));
#168272=CARTESIAN_POINT('Ctrl Pts',(-18.7781807533269,-21.0688165496486,
18.1155496590693));
#168273=CARTESIAN_POINT('Ctrl Pts',(-18.688839464362,-21.0692343228054,
18.1099964427806));
#168274=CARTESIAN_POINT('Ctrl Pts',(-18.633794657651,-21.0673436415773,
18.1065104013983));
#168275=CARTESIAN_POINT('Ctrl Pts',(-18.4698251969851,-21.0552973934552,
18.0959428714677));
#168276=CARTESIAN_POINT('Ctrl Pts',(-18.3615529979198,-21.0388464283819,
18.0887129854226));
#168277=CARTESIAN_POINT('Ctrl Pts',(-18.2114912298976,-21.0039924234121,
18.0785363688311));
#168278=CARTESIAN_POINT('Ctrl Pts',(-18.1682672901211,-20.9924987130141,
18.0755880089385));
#168279=CARTESIAN_POINT('Ctrl Pts',(-18.1012772324308,-20.9723928515956,
18.0710175203661));
#168280=CARTESIAN_POINT('Ctrl Pts',(-18.0772463794659,-20.9647096482502,
18.0693778409696));
#168281=CARTESIAN_POINT('Ctrl Pts',(-18.0061316575159,-20.9405633327487,
18.0645353213173));
#168282=CARTESIAN_POINT('Ctrl Pts',(-17.9594824762451,-20.9228627359995,
18.0613715088615));
#168283=CARTESIAN_POINT('Ctrl Pts',(-17.9062943651239,-20.9005003091176,
18.0578132958856));
#168284=CARTESIAN_POINT('Ctrl Pts',(-17.899107000947,-20.8974315092235,
18.057333533971));
#168285=CARTESIAN_POINT('Ctrl Pts',(-17.8876573644764,-20.8924677007372,
18.0565711557512));
#168286=CARTESIAN_POINT('Ctrl Pts',(-17.8833841550521,-20.8905983182683,
18.0562870459428));
#168287=CARTESIAN_POINT('Ctrl Pts',(-17.8758323811237,-20.8872648990781,
18.0557857526248));
#168288=CARTESIAN_POINT('Ctrl Pts',(-17.8725513201089,-20.8858066253754,
18.0555682214023));
#168289=CARTESIAN_POINT('Ctrl Pts',(-17.8656110037712,-20.8827008196495,
18.0551086682571));
#168290=CARTESIAN_POINT('Ctrl Pts',(-17.8619527254979,-20.8810512319314,
18.0548667747834));
#168291=CARTESIAN_POINT('Ctrl Pts',(-17.8521058793528,-20.8765773650674,
18.0542165376706));
#168292=CARTESIAN_POINT('Ctrl Pts',(-17.8459261362952,-20.8737336156806,
18.053809374079));
#168293=CARTESIAN_POINT('Ctrl Pts',(-17.8155051845937,-20.8595566422519,
18.0518090478888));
#168294=CARTESIAN_POINT('Ctrl Pts',(-17.7914654681454,-20.847793732554,
18.0502409302592));
#168295=CARTESIAN_POINT('Ctrl Pts',(-17.7228371599742,-20.8125848346542,
18.0457826621028));
#168296=CARTESIAN_POINT('Ctrl Pts',(-17.6788521079625,-20.7879983166106,
18.0429479230668));
#168297=CARTESIAN_POINT('Ctrl Pts',(-17.5228299208417,-20.6933248420271,
18.0328274459526));
#168298=CARTESIAN_POINT('Ctrl Pts',(-17.4165383533822,-20.6143604956974,
18.0257891302147));
#168299=CARTESIAN_POINT('Ctrl Pts',(-17.2410217493351,-20.4564957652909,
18.0128026653224));
#168300=CARTESIAN_POINT('Ctrl Pts',(-17.1689780628106,-20.3814033227774,
18.0069635370779));
#168301=CARTESIAN_POINT('Ctrl Pts',(-17.0937841342084,-20.2904986119138,
18.0000501285924));
#168302=CARTESIAN_POINT('Ctrl Pts',(-17.0849323036247,-20.2795776207272,
17.9992221052818));
#168303=CARTESIAN_POINT('Ctrl Pts',(-17.0709740091984,-20.2620014883353,
17.997893082113));
#168304=CARTESIAN_POINT('Ctrl Pts',(-17.065797102752,-20.2554026377321,
17.9973949032759));
#168305=CARTESIAN_POINT('Ctrl Pts',(-17.0567111208458,-20.2436781975901,
17.9965110825607));
#168306=CARTESIAN_POINT('Ctrl Pts',(-17.0527859649435,-20.2385651624284,
17.9961260845979));
#168307=CARTESIAN_POINT('Ctrl Pts',(-17.0446916909445,-20.2279210050911,
17.9953254697914));
#168308=CARTESIAN_POINT('Ctrl Pts',(-17.0405262489611,-20.2223871957183,
17.9949097148293));
#168309=CARTESIAN_POINT('Ctrl Pts',(-17.0298535752569,-20.2080627301401,
17.9938346897126));
#168310=CARTESIAN_POINT('Ctrl Pts',(-17.0233872356521,-20.1992419903254,
17.9931738370211));
#168311=CARTESIAN_POINT('Ctrl Pts',(-16.9962582801869,-20.1616275171632,
17.9903601918649));
#168312=CARTESIAN_POINT('Ctrl Pts',(-16.9762530581476,-20.1323687835299,
17.9881823815818));
#168313=CARTESIAN_POINT('Ctrl Pts',(-16.9256642718921,-20.0542401112198,
17.9823914183201));
#168314=CARTESIAN_POINT('Ctrl Pts',(-16.896327505035,-20.0046016523789,
17.9787356803089));
#168315=CARTESIAN_POINT('Ctrl Pts',(-16.7931618785148,-19.8125550916975,
17.9646949379143));
#168316=CARTESIAN_POINT('Ctrl Pts',(-16.7335762438135,-19.6631294708399,
17.953928257806));
#168317=CARTESIAN_POINT('Ctrl Pts',(-16.6876722885981,-19.4946199940057,
17.942569155782));
#168318=CARTESIAN_POINT('Ctrl Pts',(-16.6840529924436,-19.4807824131925,
17.9416423151621));
#168319=CARTESIAN_POINT('Ctrl Pts',(-16.678091015169,-19.4570064089786,
17.9400610435645));
#168320=CARTESIAN_POINT('Ctrl Pts',(-16.6756795120582,-19.4470858530889,
17.9394045915666));
#168321=CARTESIAN_POINT('Ctrl Pts',(-16.6639027907777,-19.3970643846387,
17.9361125930817));
#168322=CARTESIAN_POINT('Ctrl Pts',(-16.655636573956,-19.3567106947001,
17.9335146964976));
#168323=CARTESIAN_POINT('Ctrl Pts',(-16.6472805078279,-19.3088549163633,
17.930521480672));
#168324=CARTESIAN_POINT('Ctrl Pts',(-16.6460468456,-19.3015644419097,17.9300678722536));
#168325=CARTESIAN_POINT('Ctrl Pts',(-16.6441094919014,-19.2897391315461,
17.9293361378908));
#168326=CARTESIAN_POINT('Ctrl Pts',(-16.6433823163802,-19.2852082812151,
17.929056731494));
#168327=CARTESIAN_POINT('Ctrl Pts',(-16.6421152128537,-19.2771458141817,
17.9285612830895));
#168328=CARTESIAN_POINT('Ctrl Pts',(-16.6415694877184,-19.273615166166,
17.928344916689));
#168329=CARTESIAN_POINT('Ctrl Pts',(-16.640415942359,-19.2660249077274,
17.9278810572489));
#168330=CARTESIAN_POINT('Ctrl Pts',(-16.6398109924286,-19.261964917865,
17.9276337277719));
#168331=CARTESIAN_POINT('Ctrl Pts',(-16.6381749599386,-19.2507615954838,
17.9269533405965));
#168332=CARTESIAN_POINT('Ctrl Pts',(-16.6371685812266,-19.243614632934,
17.9265216579451));
#168333=CARTESIAN_POINT('Ctrl Pts',(-16.6318742691093,-19.2045711290714,
17.9241755801043));
#168334=CARTESIAN_POINT('Ctrl Pts',(-16.6282773117048,-19.1725832672436,
17.9222977985801));
#168335=CARTESIAN_POINT('Ctrl Pts',(-16.6108971997941,-18.9781914165722,
17.9110876207304));
#168336=CARTESIAN_POINT('Ctrl Pts',(-16.615176113916,-18.8147090529558,
17.9024736817256));
#168337=CARTESIAN_POINT('Ctrl Pts',(-16.6546729276598,-18.5375589534647,
17.8871483232951));
#168338=CARTESIAN_POINT('Ctrl Pts',(-16.6807308552497,-18.423376311942,
17.8806207754489));
#168339=CARTESIAN_POINT('Ctrl Pts',(-16.7203991369298,-18.2983144447326,
17.872934518568));
#168340=CARTESIAN_POINT('Ctrl Pts',(-16.7248577776747,-18.2847363665848,
17.8720929300055));
#168341=CARTESIAN_POINT('Ctrl Pts',(-16.7321725086049,-18.2631987343387,
17.8707462452477));
#168342=CARTESIAN_POINT('Ctrl Pts',(-16.7349394521248,-18.2552092052508,
17.8702440909771));
#168343=CARTESIAN_POINT('Ctrl Pts',(-16.7399036960803,-18.2411479604066,
17.8693556510027));
#168344=CARTESIAN_POINT('Ctrl Pts',(-16.7420810653653,-18.2350692865287,
17.8689700314587));
#168345=CARTESIAN_POINT('Ctrl Pts',(-16.7466420067172,-18.2225174510772,
17.8681705208135));
#168346=CARTESIAN_POINT('Ctrl Pts',(-16.7490294738545,-18.2160457954264,
17.8677565034186));
#168347=CARTESIAN_POINT('Ctrl Pts',(-16.7552388514241,-18.199464197434,
17.8666910436713));
#168348=CARTESIAN_POINT('Ctrl Pts',(-16.7591065991258,-18.1893717382264,
17.8660380720966));
#168349=CARTESIAN_POINT('Ctrl Pts',(-16.7755712363579,-18.1473743888241,
17.8633018602378));
#168350=CARTESIAN_POINT('Ctrl Pts',(-16.7888647574681,-18.115749876861,
17.8611952853886));
#168351=CARTESIAN_POINT('Ctrl Pts',(-16.8254985865632,-18.0342053379851,
17.8556386846199));
#168352=CARTESIAN_POINT('Ctrl Pts',(-16.8500288197882,-17.9848513773637,
17.852150236659));
#168353=CARTESIAN_POINT('Ctrl Pts',(-16.9289261427216,-17.840531026078,
17.8415780836179));
#168354=CARTESIAN_POINT('Ctrl Pts',(-16.9887548601632,-17.7487665039285,
17.8343459963911));
#168355=CARTESIAN_POINT('Ctrl Pts',(-17.0844199624271,-17.6242790132634,
17.8239750033247));
#168356=CARTESIAN_POINT('Ctrl Pts',(-17.1147074189003,-17.5875040936933,
17.8208350019414));
#168357=CARTESIAN_POINT('Ctrl Pts',(-17.1586751012275,-17.5376465687959,
17.8164967139863));
#168358=CARTESIAN_POINT('Ctrl Pts',(-17.1713284933177,-17.5236786227049,
17.8152719797419));
#168359=CARTESIAN_POINT('Ctrl Pts',(-17.2202940475182,-17.4710557495798,
17.8106273512723));
#168360=CARTESIAN_POINT('Ctrl Pts',(-17.2578707559631,-17.4335978599135,
17.8072566589758));
#168361=CARTESIAN_POINT('Ctrl Pts',(-17.3032078547312,-17.3916799780263,
17.8034478289373));
#168362=CARTESIAN_POINT('Ctrl Pts',(-17.3096341987788,-17.3858113765512,
17.8029137080426));
#168363=CARTESIAN_POINT('Ctrl Pts',(-17.3194229320678,-17.3769822909379,
17.8021090595249));
#168364=CARTESIAN_POINT('Ctrl Pts',(-17.3227587389416,-17.3739926587881,
17.8018364052111));
#168365=CARTESIAN_POINT('Ctrl Pts',(-17.3287654079445,-17.3686436152918,
17.8013482697657));
#168366=CARTESIAN_POINT('Ctrl Pts',(-17.3314327487049,-17.366280350793,
17.8011325017971));
#168367=CARTESIAN_POINT('Ctrl Pts',(-17.3372437551414,-17.3611579314137,
17.8006645969034));
#168368=CARTESIAN_POINT('Ctrl Pts',(-17.340389624003,-17.3584013631583,
17.8004126520303));
#168369=CARTESIAN_POINT('Ctrl Pts',(-17.349254687633,-17.3506796758451,
17.7997064207209));
#168370=CARTESIAN_POINT('Ctrl Pts',(-17.354992453285,-17.3457358403098,
17.7992536868585));
#168371=CARTESIAN_POINT('Ctrl Pts',(-17.3895684469105,-17.3162659276918,
17.796550677727));
#168372=CARTESIAN_POINT('Ctrl Pts',(-17.4190357323694,-17.2924845491952,
17.7943514251423));
#168373=CARTESIAN_POINT('Ctrl Pts',(-17.5183858672402,-17.2166137233403,
17.7872144816035));
#168374=CARTESIAN_POINT('Ctrl Pts',(-17.5908502661414,-17.1680453090892,
17.7824434024078));
#168375=CARTESIAN_POINT('Ctrl Pts',(-17.817451341929,-17.0356623226124,
17.768164453403));
#168376=CARTESIAN_POINT('Ctrl Pts',(-17.9791705065439,-16.9663924702893,
17.7587402039719));
#168377=CARTESIAN_POINT('Ctrl Pts',(-18.1696788833234,-16.9114706480384,
17.7472193808982));
#168378=CARTESIAN_POINT('Ctrl Pts',(-18.1918880846909,-16.9054582903882,
17.7458714707137));
#168379=CARTESIAN_POINT('Ctrl Pts',(-18.2234468138566,-16.8974646205239,
17.7439475629521));
#168380=CARTESIAN_POINT('Ctrl Pts',(-18.2327190215832,-16.89518266306,17.7433812692646));
#168381=CARTESIAN_POINT('Ctrl Pts',(-18.2478102018781,-16.8915767207952,
17.7424577892536));
#168382=CARTESIAN_POINT('Ctrl Pts',(-18.253619958686,-16.8902144573037,
17.7421018397939));
#168383=CARTESIAN_POINT('Ctrl Pts',(-18.2657935338122,-16.8874142617773,
17.7413550601512));
#168384=CARTESIAN_POINT('Ctrl Pts',(-18.2721583863564,-16.8859811501632,
17.7409640793353));
#168385=CARTESIAN_POINT('Ctrl Pts',(-18.2873166923117,-16.8826416498728,
17.7400316206717));
#168386=CARTESIAN_POINT('Ctrl Pts',(-18.2961158216974,-16.8807618676034,
17.7394892961804));
#168387=CARTESIAN_POINT('Ctrl Pts',(-18.3258040470608,-16.8746171259111,
17.7376558202103));
#168388=CARTESIAN_POINT('Ctrl Pts',(-18.3467449882263,-16.8706117504819,
17.7363564238879));
#168389=CARTESIAN_POINT('Ctrl Pts',(-18.3967051818417,-16.8618359061918,
17.733240835881));
#168390=CARTESIAN_POINT('Ctrl Pts',(-18.4257697594218,-16.8573526029304,
17.7314159076659));
#168391=CARTESIAN_POINT('Ctrl Pts',(-18.6240074188167,-16.8309889644209,
17.7188822044678));
#168392=CARTESIAN_POINT('Ctrl Pts',(-18.7951749858893,-16.8290242793281,
17.7075589997895));
#168393=CARTESIAN_POINT('Ctrl Pts',(-19.0639324695801,-16.8584857817227,
17.6897454203541));
#168394=CARTESIAN_POINT('Ctrl Pts',(-19.1622974466557,-16.8763740102327,
17.6832372934216));
#168395=CARTESIAN_POINT('Ctrl Pts',(-19.2684333813919,-16.9035459636881,
17.6764682477308));
#168396=CARTESIAN_POINT('Ctrl Pts',(-19.2778083110832,-16.906014783282,
17.6758726031909));
#168397=CARTESIAN_POINT('Ctrl Pts',(-19.2916250249826,-16.909754992671,
17.6749984298098));
#168398=CARTESIAN_POINT('Ctrl Pts',(-19.2960799832256,-16.9109766214377,
17.6747171354141));
#168399=CARTESIAN_POINT('Ctrl Pts',(-19.3039761860761,-16.9131697146314,
17.6742196066378));
#168400=CARTESIAN_POINT('Ctrl Pts',(-19.3074190003406,-16.9141353244245,
17.6740030374042));
#168401=CARTESIAN_POINT('Ctrl Pts',(-19.3147899559618,-16.9162228228039,
17.6735401463265));
#168402=CARTESIAN_POINT('Ctrl Pts',(-19.3187172904802,-16.9173473566721,
17.6732939806903));
#168403=CARTESIAN_POINT('Ctrl Pts',(-19.3294884085617,-16.9204652684806,
17.6726200705718));
#168404=CARTESIAN_POINT('Ctrl Pts',(-19.3363254905344,-16.9224818757044,
17.6721936581587));
#168405=CARTESIAN_POINT('Ctrl Pts',(-19.3727667734363,-16.9334306575288,
17.6699275260774));
#168406=CARTESIAN_POINT('Ctrl Pts',(-19.4021844545463,-16.9429766196145,
17.6681215376675));
#168407=CARTESIAN_POINT('Ctrl Pts',(-19.4905803396192,-16.9738175161009,
17.662736428932));
#168408=CARTESIAN_POINT('Ctrl Pts',(-19.548834371254,-16.9970918574056,
17.6592440442081));
#168409=CARTESIAN_POINT('Ctrl Pts',(-19.7460347906743,-17.0862293796931,
17.6473504516521));
#168410=CARTESIAN_POINT('Ctrl Pts',(-19.8787811477698,-17.1646021563576,
17.6391831377827));
#168411=CARTESIAN_POINT('Ctrl Pts',(-20.0057612100994,-17.2595650699986,
17.6302909514503));
#168412=CARTESIAN_POINT('Ctrl Pts',(-20.0096389099454,-17.2624858867679,
17.6300183180715));
#168413=CARTESIAN_POINT('Ctrl Pts',(-20.0639398701358,-17.3036807498926,
17.6261849813003));
#168414=CARTESIAN_POINT('Ctrl Pts',(-20.1126276207476,-17.3441812369468,
17.6225577387224));
#168415=CARTESIAN_POINT('Ctrl Pts',(-20.1686735537514,-17.3952221498228,
17.6181060949458));
#168416=CARTESIAN_POINT('Ctrl Pts',(-20.177847238413,-17.4037265672025,
17.617368124686));
#168417=CARTESIAN_POINT('Ctrl Pts',(-20.1927722300276,-17.417810709638,
17.6161517888953));
#168418=CARTESIAN_POINT('Ctrl Pts',(-20.1985682625042,-17.4233427462219,
17.6156754718345));
#168419=CARTESIAN_POINT('Ctrl Pts',(-20.2089226982498,-17.4333385050625,
17.6148173198028));
#168420=CARTESIAN_POINT('Ctrl Pts',(-20.2134926128986,-17.4377902031027,
17.6144360111681));
#168421=CARTESIAN_POINT('Ctrl Pts',(-20.2223064923953,-17.4464540731883,
17.6136955645564));
#168422=CARTESIAN_POINT('Ctrl Pts',(-20.2265528757389,-17.4506637068841,
17.6133365402136));
#168423=CARTESIAN_POINT('Ctrl Pts',(-20.2380573690419,-17.4621656840978,
17.6123575628236));
#168424=CARTESIAN_POINT('Ctrl Pts',(-20.2452801728556,-17.4694929708463,
17.6117360590886));
#168425=CARTESIAN_POINT('Ctrl Pts',(-20.274574021194,-17.4996471239514,
17.6091868388208));
#168426=CARTESIAN_POINT('Ctrl Pts',(-20.2961826748662,-17.5229155693371,
17.607239247281));
#168427=CARTESIAN_POINT('Ctrl Pts',(-20.3503819733628,-17.5839766223115,
17.6021747762768));
#168428=CARTESIAN_POINT('Ctrl Pts',(-20.3821730448234,-17.6224498355758,
17.5990270878846));
#168429=CARTESIAN_POINT('Ctrl Pts',(-20.4577559662583,-17.7208004266969,
17.5910890524617));
#168430=CARTESIAN_POINT('Ctrl Pts',(-20.4998152237406,-17.7819221384846,
17.5862481251173));
#168431=CARTESIAN_POINT('Ctrl Pts',(-20.6124795016572,-17.9656020308039,
17.5720556264622));
#168432=CARTESIAN_POINT('Ctrl Pts',(-20.6741167587004,-18.0931629493534,
17.5626093903388));
#168433=CARTESIAN_POINT('Ctrl Pts',(-20.7225805855593,-18.2258896401121,
17.5536949999931));
#168434=CARTESIAN_POINT('Ctrl Pts',(-20.7225805737356,-18.2258896077308,
17.3329786086887));
#168435=CARTESIAN_POINT('Ctrl Pts',(-20.7104864421468,-18.1927677086508,
17.3349098494595));
#168436=CARTESIAN_POINT('Ctrl Pts',(-20.6975577347975,-18.1599286202259,
17.3368537579916));
#168437=CARTESIAN_POINT('Ctrl Pts',(-20.6624014074273,-18.0767995408689,
17.34187307398));
#168438=CARTESIAN_POINT('Ctrl Pts',(-20.6390395045528,-18.0270504459731,
17.3449716029928));
#168439=CARTESIAN_POINT('Ctrl Pts',(-20.5980248124357,-17.9478723399229,
17.3501020614207));
#168440=CARTESIAN_POINT('Ctrl Pts',(-20.5815450858772,-17.9178637326673,
17.3520948747823));
#168441=CARTESIAN_POINT('Ctrl Pts',(-20.5589189004514,-17.8789311986134,
17.3547506063541));
#168442=CARTESIAN_POINT('Ctrl Pts',(-20.5534207804574,-17.8696351526262,
17.3553901070576));
#168443=CARTESIAN_POINT('Ctrl Pts',(-20.5442958218112,-17.8544729633609,
17.3564421940304));
#168444=CARTESIAN_POINT('Ctrl Pts',(-20.540710980588,-17.8485816797273,
17.3568532425771));
#168445=CARTESIAN_POINT('Ctrl Pts',(-20.533713716258,-17.8372079834685,
17.3576512477811));
#168446=CARTESIAN_POINT('Ctrl Pts',(-20.5303048638004,-17.8317234558095,
17.3580380698636));
#168447=CARTESIAN_POINT('Ctrl Pts',(-20.5223725887378,-17.8190904513582,
17.3589337820094));
#168448=CARTESIAN_POINT('Ctrl Pts',(-20.5178313280707,-17.8119533556468,
17.3594433297405));
#168449=CARTESIAN_POINT('Ctrl Pts',(-20.5054952879657,-17.7928200701284,
17.3608189157874));
#168450=CARTESIAN_POINT('Ctrl Pts',(-20.4976215864081,-17.7808755193036,
17.3616878906464));
#168451=CARTESIAN_POINT('Ctrl Pts',(-20.4088268220344,-17.6490985903593,
17.3713906080218));
#168452=CARTESIAN_POINT('Ctrl Pts',(-20.3159688849382,-17.5378016068516,
17.3806984685398));
#168453=CARTESIAN_POINT('Ctrl Pts',(-20.1259489280883,-17.3523759933019,
17.3981791058077));
#168454=CARTESIAN_POINT('Ctrl Pts',(-20.0322997581734,-17.2754743683484,
17.4062464900393));
#168455=CARTESIAN_POINT('Ctrl Pts',(-19.9076880640577,-17.189882445696,
17.4159558849985));
#168456=CARTESIAN_POINT('Ctrl Pts',(-19.8824175958746,-17.1733097068011,
17.4178758980935));
#168457=CARTESIAN_POINT('Ctrl Pts',(-19.8462044475652,-17.1506542626023,
17.4205498398584));
#168458=CARTESIAN_POINT('Ctrl Pts',(-19.8355503603132,-17.1441194678071,
17.4213272722956));
#168459=CARTESIAN_POINT('Ctrl Pts',(-19.8191315180389,-17.1342478343637,
17.4225105122093));
#168460=CARTESIAN_POINT('Ctrl Pts',(-19.8134080365084,-17.1308433234689,
17.4229202450091));
#168461=CARTESIAN_POINT('Ctrl Pts',(-19.8039353093024,-17.1252689862117,
17.4235937542175));
#168462=CARTESIAN_POINT('Ctrl Pts',(-19.8001953462669,-17.1230835866061,
17.4238584827382));
#168463=CARTESIAN_POINT('Ctrl Pts',(-19.7929546010434,-17.1188823083169,
17.4243686892573));
#168464=CARTESIAN_POINT('Ctrl Pts',(-19.7894547080002,-17.116864942675,
17.4246142607741));
#168465=CARTESIAN_POINT('Ctrl Pts',(-19.7829360499672,-17.1131323545322,
17.4250696789485));
#168466=CARTESIAN_POINT('Ctrl Pts',(-19.7799188699792,-17.11141455723,17.425279687199));
#168467=CARTESIAN_POINT('Ctrl Pts',(-19.7729869984992,-17.1074905236333,
17.4257603926587));
#168468=CARTESIAN_POINT('Ctrl Pts',(-19.7690695086505,-17.1052893284072,
17.4260307642412));
#168469=CARTESIAN_POINT('Ctrl Pts',(-19.7574873619518,-17.0988298787264,
17.426826397402));
#168470=CARTESIAN_POINT('Ctrl Pts',(-19.7498031172166,-17.0946066890604,
17.4273494661493));
#168471=CARTESIAN_POINT('Ctrl Pts',(-19.6942554725164,-17.0645260506725,
17.4310977695132));
#168472=CARTESIAN_POINT('Ctrl Pts',(-19.645433006508,-17.0404719642183,
17.4342175375556));
#168473=CARTESIAN_POINT('Ctrl Pts',(-19.459347146141,-16.9575436709873,
17.4456647095087));
#168474=CARTESIAN_POINT('Ctrl Pts',(-19.3169061446843,-16.9113602014049,
17.4535772797177));
#168475=CARTESIAN_POINT('Ctrl Pts',(-19.0759200610691,-16.8605462661092,
17.4671151405275));
#168476=CARTESIAN_POINT('Ctrl Pts',(-18.9798058060513,-16.8470856630991,
17.4725462891269));
#168477=CARTESIAN_POINT('Ctrl Pts',(-18.8615918994072,-16.8387383429261,
17.4794457055602));
#168478=CARTESIAN_POINT('Ctrl Pts',(-18.8400481220496,-16.8375477614194,
17.4807115638795));
#168479=CARTESIAN_POINT('Ctrl Pts',(-18.8094568186734,-16.8363258744036,
17.4825224785959));
#168480=CARTESIAN_POINT('Ctrl Pts',(-18.8004210491932,-16.8360229260303,
17.4830590294245));
#168481=CARTESIAN_POINT('Ctrl Pts',(-18.7848540245107,-16.835600808806,
17.4839863754321));
#168482=CARTESIAN_POINT('Ctrl Pts',(-18.7783236000857,-16.8354539727905,
17.4843762985894));
#168483=CARTESIAN_POINT('Ctrl Pts',(-18.765835113166,-16.8352309929499,
17.4851237266227));
#168484=CARTESIAN_POINT('Ctrl Pts',(-18.7598771952045,-16.8351497754261,
17.4854810686031));
#168485=CARTESIAN_POINT('Ctrl Pts',(-18.7444196032331,-16.8350043269884,
17.4864101986601));
#168486=CARTESIAN_POINT('Ctrl Pts',(-18.7349197754839,-16.8349788860067,
17.486983196933));
#168487=CARTESIAN_POINT('Ctrl Pts',(-18.7027105527993,-16.8351094246879,
17.4889328328188));
#168488=CARTESIAN_POINT('Ctrl Pts',(-18.6800045690789,-16.8355668761448,
17.4903188547222));
#168489=CARTESIAN_POINT('Ctrl Pts',(-18.4783258766554,-16.842877548468,
17.50273725856));
#168490=CARTESIAN_POINT('Ctrl Pts',(-18.3009195556806,-16.8720521078611,
17.514506601087));
#168491=CARTESIAN_POINT('Ctrl Pts',(-18.0483550700515,-16.947324988999,
17.5319155793778));
#168492=CARTESIAN_POINT('Ctrl Pts',(-17.9688784480643,-16.9762920940486,
17.5374791670365));
#168493=CARTESIAN_POINT('Ctrl Pts',(-17.8572323808124,-17.0247350824564,
17.5452450742251));
#168494=CARTESIAN_POINT('Ctrl Pts',(-17.8235159660938,-17.0404323879336,
17.5475829398941));
#168495=CARTESIAN_POINT('Ctrl Pts',(-17.7834837272261,-17.0603698596369,
17.5503347481257));
#168496=CARTESIAN_POINT('Ctrl Pts',(-17.7767569975213,-17.0637649481949,
17.5507963096006));
#168497=CARTESIAN_POINT('Ctrl Pts',(-17.7663320408895,-17.069096618253,
17.5515101634834));
#168498=CARTESIAN_POINT('Ctrl Pts',(-17.7626212516536,-17.0710083062281,
17.5517639713802));
#168499=CARTESIAN_POINT('Ctrl Pts',(-17.7557522885665,-17.0745727390417,
17.5522332166924));
#168500=CARTESIAN_POINT('Ctrl Pts',(-17.7525926627584,-17.0762224695307,
17.5524488333306));
#168501=CARTESIAN_POINT('Ctrl Pts',(-17.7454618917507,-17.0799685973449,
17.5529349387837));
#168502=CARTESIAN_POINT('Ctrl Pts',(-17.741493251985,-17.0820696483594,
17.5532051290437));
#168503=CARTESIAN_POINT('Ctrl Pts',(-17.7298078531374,-17.0883037368409,
17.5539997343143));
#168504=CARTESIAN_POINT('Ctrl Pts',(-17.7221099010328,-17.0924720860575,
17.5545219649416));
#168505=CARTESIAN_POINT('Ctrl Pts',(-17.6669813545786,-17.1227672505914,
17.5582546395922));
#168506=CARTESIAN_POINT('Ctrl Pts',(-17.6205384994342,-17.1506600016381,
17.5613605901472));
#168507=CARTESIAN_POINT('Ctrl Pts',(-17.435217856908,-17.2718700897137,
17.5738056069297));
#168508=CARTESIAN_POINT('Ctrl Pts',(-17.3065629186422,-17.3797078871075,
17.5826127482353));
#168509=CARTESIAN_POINT('Ctrl Pts',(-17.1508616628789,-17.5452460902517,
17.5952017838381));
#168510=CARTESIAN_POINT('Ctrl Pts',(-17.1116611892639,-17.5906405533614,
17.5985705487878));
#168511=CARTESIAN_POINT('Ctrl Pts',(-17.0518068099685,-17.6662145567908,
17.6041067593827));
#168512=CARTESIAN_POINT('Ctrl Pts',(-17.0299149798136,-17.6953727107602,
17.606226459287));
#168513=CARTESIAN_POINT('Ctrl Pts',(-17.0023843709895,-17.7340844073729,
17.6090269959459));
#168514=CARTESIAN_POINT('Ctrl Pts',(-16.9960516197295,-17.7431383462476,
17.6096810293439));
#168515=CARTESIAN_POINT('Ctrl Pts',(-16.9858508129245,-17.7579682851499,
17.6107509427807));
#168516=CARTESIAN_POINT('Ctrl Pts',(-16.9819397704358,-17.7637145685701,
17.6111651815024));
#168517=CARTESIAN_POINT('Ctrl Pts',(-16.9744614332803,-17.7748192706471,
17.6119651152198));
#168518=CARTESIAN_POINT('Ctrl Pts',(-16.9708901353176,-17.7801749102472,
17.6123506529619));
#168519=CARTESIAN_POINT('Ctrl Pts',(-16.9627530154023,-17.7924990188325,
17.6132372819855));
#168520=CARTESIAN_POINT('Ctrl Pts',(-16.9582038125271,-17.7994782851359,
17.6137389890164));
#168521=CARTESIAN_POINT('Ctrl Pts',(-16.9461933422388,-17.8181443634005,
17.6150798397191));
#168522=CARTESIAN_POINT('Ctrl Pts',(-16.9388055900956,-17.8298777845196,
17.6159216937581));
#168523=CARTESIAN_POINT('Ctrl Pts',(-16.8813286698825,-17.9231846341802,
17.62260948816));
#168524=CARTESIAN_POINT('Ctrl Pts',(-16.8367161307349,-18.0079864276178,
17.6286545164905));
#168525=CARTESIAN_POINT('Ctrl Pts',(-16.7419254054438,-18.2222494063162,
17.6438220640093));
#168526=CARTESIAN_POINT('Ctrl Pts',(-16.6984367933057,-18.354191151171,
17.6530889356279));
#168527=CARTESIAN_POINT('Ctrl Pts',(-16.6568246718478,-18.5400277691299,
17.6655380253888));
#168528=CARTESIAN_POINT('Ctrl Pts',(-16.6473555017964,-18.5910375014303,
17.6688914276431));
#168529=CARTESIAN_POINT('Ctrl Pts',(-16.6357771673603,-18.6693434832353,
17.673895446549));
#168530=CARTESIAN_POINT('Ctrl Pts',(-16.6323075896126,-18.6964164758954,
17.6755994724613));
#168531=CARTESIAN_POINT('Ctrl Pts',(-16.6286234454546,-18.7303573949368,
17.6776970526797));
#168532=CARTESIAN_POINT('Ctrl Pts',(-16.6279175931669,-18.7371680205407,
17.6781160103822));
#168533=CARTESIAN_POINT('Ctrl Pts',(-16.6268494987093,-18.7479854218743,
17.6787782305216));
#168534=CARTESIAN_POINT('Ctrl Pts',(-16.6264656204226,-18.7519899435012,
17.6790226806623));
#168535=CARTESIAN_POINT('Ctrl Pts',(-16.6257609426452,-18.7595683188277,
17.6794839382517));
#168536=CARTESIAN_POINT('Ctrl Pts',(-16.6254378183752,-18.7631418488362,
17.6797008682422));
#168537=CARTESIAN_POINT('Ctrl Pts',(-16.6247171124215,-18.7713448333614,
17.680197536256));
#168538=CARTESIAN_POINT('Ctrl Pts',(-16.6243256855282,-18.7759747834404,
17.6804769261422));
#168539=CARTESIAN_POINT('Ctrl Pts',(-16.623321711021,-18.7883348272222,
17.681220359968));
#168540=CARTESIAN_POINT('Ctrl Pts',(-16.6227363791084,-18.7960671438983,
17.6816829187391));
#168541=CARTESIAN_POINT('Ctrl Pts',(-16.6188025926289,-18.8521234424839,
17.6850191174309));
#168542=CARTESIAN_POINT('Ctrl Pts',(-16.6170708242361,-18.9005505293486,
17.6878089138649));
#168543=CARTESIAN_POINT('Ctrl Pts',(-16.6169630320092,-18.9765706720492,
17.692102262049));
#168544=CARTESIAN_POINT('Ctrl Pts',(-16.6174626075037,-19.0041421183956,
17.6936416334007));
#168545=CARTESIAN_POINT('Ctrl Pts',(-16.6201528146951,-19.0755519656355,
17.6975997228564));
#168546=CARTESIAN_POINT('Ctrl Pts',(-16.6231683181137,-19.1193464267854,
17.6999990458829));
#168547=CARTESIAN_POINT('Ctrl Pts',(-16.6384409340647,-19.2718041924397,
17.7083409402699));
#168548=CARTESIAN_POINT('Ctrl Pts',(-16.6577499340344,-19.3795830892136,
17.7142281680917));
#168549=CARTESIAN_POINT('Ctrl Pts',(-16.7043608332299,-19.5586134350395,
17.724514928789));
#168550=CARTESIAN_POINT('Ctrl Pts',(-16.727336922796,-19.6307610478067,
17.7288045190204));
#168551=CARTESIAN_POINT('Ctrl Pts',(-16.7608127270424,-19.7191883226073,
17.7343248003963));
#168552=CARTESIAN_POINT('Ctrl Pts',(-16.7677377274275,-19.7367665753161,
17.7354353641098));
#168553=CARTESIAN_POINT('Ctrl Pts',(-16.7781445529553,-19.7621801743971,
17.7370611884304));
#168554=CARTESIAN_POINT('Ctrl Pts',(-16.7814402907764,-19.7700910849917,
17.7375701641849));
#168555=CARTESIAN_POINT('Ctrl Pts',(-16.787301175385,-19.7839220581577,
17.7384651761504));
#168556=CARTESIAN_POINT('Ctrl Pts',(-16.7898455360463,-19.7898508479875,
17.7388505012132));
#168557=CARTESIAN_POINT('Ctrl Pts',(-16.7948374900136,-19.8013377671802,
17.7396003458106));
#168558=CARTESIAN_POINT('Ctrl Pts',(-16.7972819800069,-19.8068971825513,
17.739964756213));
#168559=CARTESIAN_POINT('Ctrl Pts',(-16.8031808943796,-19.8201577168425,
17.7408375942988));
#168560=CARTESIAN_POINT('Ctrl Pts',(-16.8066574997269,-19.827848801652,
17.7413467803318));
#168561=CARTESIAN_POINT('Ctrl Pts',(-16.8193569630616,-19.8555012770227,
17.7431882643749));
#168562=CARTESIAN_POINT('Ctrl Pts',(-16.8288444500643,-19.8753389354907,
17.7445296614726));
#168563=CARTESIAN_POINT('Ctrl Pts',(-16.9218510373929,-20.0622704909225,
17.7573683548412));
#168564=CARTESIAN_POINT('Ctrl Pts',(-17.0268192268646,-20.2177369755839,
17.7696769687365));
#168565=CARTESIAN_POINT('Ctrl Pts',(-17.2034616585513,-20.4167317208172,
17.787242321993));
#168566=CARTESIAN_POINT('Ctrl Pts',(-17.2594428099543,-20.4730750846991,
17.7924544141475));
#168567=CARTESIAN_POINT('Ctrl Pts',(-17.3450908809074,-20.550093631775,
17.7997956008994));
#168568=CARTESIAN_POINT('Ctrl Pts',(-17.3723281792737,-20.5733642409973,
17.8020455053046));
#168569=CARTESIAN_POINT('Ctrl Pts',(-17.4059324225588,-20.6006300558802,
17.80470776851));
#168570=CARTESIAN_POINT('Ctrl Pts',(-17.4117450485827,-20.6052956174419,
17.8051642799506));
#168571=CARTESIAN_POINT('Ctrl Pts',(-17.4208374346113,-20.6125150866815,
17.8058720277955));
#168572=CARTESIAN_POINT('Ctrl Pts',(-17.4241002143388,-20.6150901444136,
17.8061247390986));
#168573=CARTESIAN_POINT('Ctrl Pts',(-17.4301764252852,-20.6198566495197,
17.8065929846737));
#168574=CARTESIAN_POINT('Ctrl Pts',(-17.4329877827856,-20.622050576558,
17.8068086916849));
#168575=CARTESIAN_POINT('Ctrl Pts',(-17.439370564266,-20.6270056723382,
17.8072963065327));
#168576=CARTESIAN_POINT('Ctrl Pts',(-17.4429452751425,-20.6297625208964,
17.807567907784));
#168577=CARTESIAN_POINT('Ctrl Pts',(-17.4535658423472,-20.6378991526213,
17.8083705281124));
#168578=CARTESIAN_POINT('Ctrl Pts',(-17.4606368025301,-20.6432462146099,
17.8088992965071));
#168579=CARTESIAN_POINT('Ctrl Pts',(-17.5135264577695,-20.6827216407256,
17.8128146302074));
#168580=CARTESIAN_POINT('Ctrl Pts',(-17.5606806517185,-20.7150303454308,
17.8160847411955));
#168581=CARTESIAN_POINT('Ctrl Pts',(-17.737338437242,-20.8258394240807,
17.8277763709364));
#168582=CARTESIAN_POINT('Ctrl Pts',(-17.8738528201643,-20.8922991633028,
17.8357920470868));
#168583=CARTESIAN_POINT('Ctrl Pts',(-18.1035142146527,-20.9750599276034,
17.8492378292061));
#168584=CARTESIAN_POINT('Ctrl Pts',(-18.1926930861591,-21.0007234428418,
17.8544436549559));
#168585=CARTESIAN_POINT('Ctrl Pts',(-18.3038460930482,-21.024944888954,
17.8610701804794));
#168586=CARTESIAN_POINT('Ctrl Pts',(-18.3244970938798,-21.0291230630333,
17.8623067194479));
#168587=CARTESIAN_POINT('Ctrl Pts',(-18.3540091854133,-21.0346368318015,
17.864082843278));
#168588=CARTESIAN_POINT('Ctrl Pts',(-18.362822130045,-21.0362255581988,
17.8646143673312));
#168589=CARTESIAN_POINT('Ctrl Pts',(-18.378065138894,-21.0388736999805,
17.8655357617358));
#168590=CARTESIAN_POINT('Ctrl Pts',(-18.3844905499111,-21.0399594363529,
17.8659247898351));
#168591=CARTESIAN_POINT('Ctrl Pts',(-18.3968182174948,-21.0419840102106,
17.8666724199752));
#168592=CARTESIAN_POINT('Ctrl Pts',(-18.4027196456649,-21.0429275556754,
17.8670308683749));
#168593=CARTESIAN_POINT('Ctrl Pts',(-18.4181095434045,-21.045321368904,
17.8679671022208));
#168594=CARTESIAN_POINT('Ctrl Pts',(-18.4276039423149,-21.0467321034362,
17.868546134905));
#168595=CARTESIAN_POINT('Ctrl Pts',(-18.4601864383012,-21.0513471503003,
17.8705383707068));
#168596=CARTESIAN_POINT('Ctrl Pts',(-18.4833170432897,-21.0542345994454,
17.8719615236971));
#168597=CARTESIAN_POINT('Ctrl Pts',(-18.6762847338172,-21.0750932844534,
17.8839119363672));
#168598=CARTESIAN_POINT('Ctrl Pts',(-18.8476462699626,-21.0728297901392,
17.8951010561562));
#168599=CARTESIAN_POINT('Ctrl Pts',(-19.1063774921774,-21.0379499887562,
17.9123531737725));
#168600=CARTESIAN_POINT('Ctrl Pts',(-19.1950597619262,-21.020158176893,
17.9183162470272));
#168601=CARTESIAN_POINT('Ctrl Pts',(-19.3196745965612,-20.9867404052281,
17.9265592915962));
#168602=CARTESIAN_POINT('Ctrl Pts',(-19.356732494316,-20.9757064821372,
17.9289921683682));
#168603=CARTESIAN_POINT('Ctrl Pts',(-19.4007095278454,-20.9612897872786,
17.9318403065271));
#168604=CARTESIAN_POINT('Ctrl Pts',(-19.4079363517236,-20.9588773858057,
17.9323070669527));
#168605=CARTESIAN_POINT('Ctrl Pts',(-19.4191196054225,-20.9550770585963,
17.9330272023617));
#168606=CARTESIAN_POINT('Ctrl Pts',(-19.4230851151679,-20.9537163338412,
17.933282135111));
#168607=CARTESIAN_POINT('Ctrl Pts',(-19.4304131744878,-20.9511774270268,
17.9337524204992));
#168608=CARTESIAN_POINT('Ctrl Pts',(-19.4337767641568,-20.9500025462919,
17.9339679589769));
#168609=CARTESIAN_POINT('Ctrl Pts',(-19.4413507606262,-20.9473355243079,
17.9344525822863));
#168610=CARTESIAN_POINT('Ctrl Pts',(-19.4455594078557,-20.9458385498973,
17.9347213765235));
#168611=CARTESIAN_POINT('Ctrl Pts',(-19.4578988445171,-20.9414054870869,
17.935508088406));
#168612=CARTESIAN_POINT('Ctrl Pts',(-19.466016537838,-20.9384328640199,
17.9360238860025));
#168613=CARTESIAN_POINT('Ctrl Pts',(-19.5224626353362,-20.9173698232454,
17.9395997175728));
#168614=CARTESIAN_POINT('Ctrl Pts',(-19.5701378628187,-20.8975657983281,
17.9425649535421));
#168615=CARTESIAN_POINT('Ctrl Pts',(-19.636926399806,-20.8669129019215,
17.9467037880634));
#168616=CARTESIAN_POINT('Ctrl Pts',(-19.6566651687567,-20.8574806578857,
17.9479250191211));
#168617=CARTESIAN_POINT('Ctrl Pts',(-19.7995540558099,-20.7864596119881,
17.9567751987166));
#168618=CARTESIAN_POINT('Ctrl Pts',(-19.9165827754788,-20.7132916122363,
17.9640985794818));
#168619=CARTESIAN_POINT('Ctrl Pts',(-20.0975672646288,-20.5739142383143,
17.9766928253087));
#168620=CARTESIAN_POINT('Ctrl Pts',(-20.1658130976267,-20.5139955191033,
17.9817933316599));
#168621=CARTESIAN_POINT('Ctrl Pts',(-20.244737861738,-20.4351702285474,
17.988292440638));
#168622=CARTESIAN_POINT('Ctrl Pts',(-20.2592564828365,-20.4202354816829,
17.9895150620323));
#168623=CARTESIAN_POINT('Ctrl Pts',(-20.2796703515502,-20.3986069334358,
17.9912746466735));
#168624=CARTESIAN_POINT('Ctrl Pts',(-20.2857476144952,-20.3920860365729,
17.9918037560683));
#168625=CARTESIAN_POINT('Ctrl Pts',(-20.29619112644,-20.3807372934515,17.9927222995741));
#168626=CARTESIAN_POINT('Ctrl Pts',(-20.3005766563314,-20.3759272971626,
17.9931109056582));
#168627=CARTESIAN_POINT('Ctrl Pts',(-20.3089521347045,-20.3666556467147,
17.9938586666956));
#168628=CARTESIAN_POINT('Ctrl Pts',(-20.3129454863746,-20.362197140582,
17.9942176725303));
#168629=CARTESIAN_POINT('Ctrl Pts',(-20.3233262549738,-20.3505078257506,
17.9951574588914));
#168630=CARTESIAN_POINT('Ctrl Pts',(-20.3296831900043,-20.3432502419594,
17.9957395052875));
#168631=CARTESIAN_POINT('Ctrl Pts',(-20.3514218849837,-20.3180866248662,
17.9977528279286));
#168632=CARTESIAN_POINT('Ctrl Pts',(-20.3665531929145,-20.2999674410712,
17.9991943389182));
#168633=CARTESIAN_POINT('Ctrl Pts',(-20.4850680329415,-20.1531271970523,
18.0108161680665));
#168634=CARTESIAN_POINT('Ctrl Pts',(-20.5733552535207,-20.0129893381239,
18.0216100156468));
#168635=CARTESIAN_POINT('Ctrl Pts',(-20.6994386073971,-19.7488857161959,
18.0409499403857));
#168636=CARTESIAN_POINT('Ctrl Pts',(-20.743899330609,-19.6289691343491,
18.049391053653));
#168637=CARTESIAN_POINT('Ctrl Pts',(-20.7804090241341,-19.4942558051151,
18.0580465438403));
#168638=CARTESIAN_POINT('Ctrl Pts',(-20.7834316356884,-19.4827176630822,
18.0587813177728));
#168639=CARTESIAN_POINT('Ctrl Pts',(-20.7875891298045,-19.4662819698134,
18.0598180620874));
#168640=CARTESIAN_POINT('Ctrl Pts',(-20.7888042692852,-19.4614052165508,
18.0601244459327));
#168641=CARTESIAN_POINT('Ctrl Pts',(-20.7908681042927,-19.4529948179474,
18.0606506488588));
#168642=CARTESIAN_POINT('Ctrl Pts',(-20.7917250853263,-19.4494632449383,
18.0608709418033));
#168643=CARTESIAN_POINT('Ctrl Pts',(-20.7933688051065,-19.4426126363481,
18.0612969665191));
#168644=CARTESIAN_POINT('Ctrl Pts',(-20.7941566162479,-19.4392939064884,
18.0615027621465));
#168645=CARTESIAN_POINT('Ctrl Pts',(-20.7962599600606,-19.4303370937807,
18.0620566247985));
#168646=CARTESIAN_POINT('Ctrl Pts',(-20.797560402491,-19.4246954465815,
18.0624038302745));
#168647=CARTESIAN_POINT('Ctrl Pts',(-20.8022980768276,-19.4037500213828,
18.063686978631));
#168648=CARTESIAN_POINT('Ctrl Pts',(-20.8055884395178,-19.3884130912177,
18.0646148752806));
#168649=CARTESIAN_POINT('Ctrl Pts',(-20.8354454595723,-19.2412904230449,
18.073416790184));
#168650=CARTESIAN_POINT('Ctrl Pts',(-20.8495760219943,-19.1072739809901,
18.0806879222332));
#168651=CARTESIAN_POINT('Ctrl Pts',(-20.850959537806,-18.9665205892282,
18.0883318492396));
#168652=CARTESIAN_POINT('Ctrl Pts',(-20.8509933270725,-18.9602331844887,
18.0886732825532));
#168653=CARTESIAN_POINT('Ctrl Pts',(-20.851133145328,-18.8081072307474,
18.0969355113093));
#168654=CARTESIAN_POINT('Ctrl Pts',(-20.8361978945779,-18.6626640240751,
18.1048962272042));
#168655=CARTESIAN_POINT('Ctrl Pts',(-20.8015323046563,-18.4963942884213,
18.1147554858428));
#168656=CARTESIAN_POINT('Ctrl Pts',(-20.796227954925,-18.4729570083998,
18.1161622683207));
#168657=CARTESIAN_POINT('Ctrl Pts',(-20.7882195557437,-18.4401743690809,
18.1181559976384));
#168658=CARTESIAN_POINT('Ctrl Pts',(-20.7858481758035,-18.4307490831353,
18.1187322497221));
#168659=CARTESIAN_POINT('Ctrl Pts',(-20.7819083814232,-18.4155335577363,
18.1196675576472));
#168660=CARTESIAN_POINT('Ctrl Pts',(-20.7803800925137,-18.4097330010024,
18.1200253122374));
#168661=CARTESIAN_POINT('Ctrl Pts',(-20.7771446746428,-18.3976615870928,
18.1207723451549));
#168662=CARTESIAN_POINT('Ctrl Pts',(-20.7754332824839,-18.391391946855,
18.1211617585408));
#168663=CARTESIAN_POINT('Ctrl Pts',(-20.7713216385888,-18.376597555618,
18.1220840563322));
#168664=CARTESIAN_POINT('Ctrl Pts',(-20.76889672323,-18.3680798392536,18.1226177386939));
#168665=CARTESIAN_POINT('Ctrl Pts',(-20.7606830652877,-18.3399013089528,
18.1243923132876));
#168666=CARTESIAN_POINT('Ctrl Pts',(-20.7546623986689,-18.3203098236069,
18.1256407462757));
#168667=CARTESIAN_POINT('Ctrl Pts',(-20.7402319475941,-18.2756714355429,
18.128519755806));
#168668=CARTESIAN_POINT('Ctrl Pts',(-20.7316376116202,-18.2506938917112,
18.1301558996124));
#168669=CARTESIAN_POINT('Ctrl Pts',(-20.7225805578636,-18.2258895642624,
18.13180632455));
#168670=CARTESIAN_POINT('Origin',(-18.734,-18.952,0.));
#168671=CARTESIAN_POINT('',(-20.7202230294519,-18.2267290932703,19.1554367770419));
#168672=CARTESIAN_POINT('',(-20.7225805608153,-18.2258895723463,18.9348455085272));
#168673=CARTESIAN_POINT('',(-20.7225805737622,-18.2258896078036,0.));
#168674=CARTESIAN_POINT('',(-20.8499619975019,-18.9538841873159,19.1109437209775));
#168675=CARTESIAN_POINT('Ctrl Pts',(-20.8499619975019,-18.9538841873159,
19.1109437209775));
#168676=CARTESIAN_POINT('Ctrl Pts',(-20.8478498472042,-18.7070537041303,
19.1257747396657));
#168677=CARTESIAN_POINT('Ctrl Pts',(-20.8034779751874,-18.4595580078992,
19.1406057583538));
#168678=CARTESIAN_POINT('Ctrl Pts',(-20.7202230294519,-18.2267290932703,
19.1554367770419));
#168679=CARTESIAN_POINT('Ctrl Pts',(-20.850999125527,-18.9539241928138,
19.1115402607454));
#168680=CARTESIAN_POINT('Ctrl Pts',(-20.8508551448554,-19.1123318916676,
19.1011622677739));
#168681=CARTESIAN_POINT('Ctrl Pts',(-20.8329326848977,-19.2702284518518,
19.0905102687625));
#168682=CARTESIAN_POINT('Ctrl Pts',(-20.7912029051883,-19.4524161307638,
19.0786804206076));
#168683=CARTESIAN_POINT('Ctrl Pts',(-20.7842844059529,-19.4800474757292,
19.0769005643253));
#168684=CARTESIAN_POINT('Ctrl Pts',(-20.7749880166316,-19.5142322698684,
19.074723505109));
#168685=CARTESIAN_POINT('Ctrl Pts',(-20.773133013378,-19.5209233394338,
19.0742985832489));
#168686=CARTESIAN_POINT('Ctrl Pts',(-20.7701454845392,-19.5314971281306,
19.0736291200915));
#168687=CARTESIAN_POINT('Ctrl Pts',(-20.7690347136989,-19.5353858674967,
19.0733833471956));
#168688=CARTESIAN_POINT('Ctrl Pts',(-20.766918738645,-19.5427141802028,
19.0729210452307));
#168689=CARTESIAN_POINT('Ctrl Pts',(-20.7659159576265,-19.5461543418567,
19.0727043853938));
#168690=CARTESIAN_POINT('Ctrl Pts',(-20.7636032678753,-19.5540139713706,
19.0722101932646));
#168691=CARTESIAN_POINT('Ctrl Pts',(-20.762287658381,-19.5584317129533,
19.0719329969515));
#168692=CARTESIAN_POINT('Ctrl Pts',(-20.758756505162,-19.5701490813827,
19.0711992300556));
#168693=CARTESIAN_POINT('Ctrl Pts',(-20.7565158944124,-19.5774411665578,
19.0707440842364));
#168694=CARTESIAN_POINT('Ctrl Pts',(-20.7405464091695,-19.628430657502,
19.0675709948821));
#168695=CARTESIAN_POINT('Ctrl Pts',(-20.7254408808252,-19.6716880002887,
19.0649279501887));
#168696=CARTESIAN_POINT('Ctrl Pts',(-20.6584791004688,-19.845142128339,
19.0544019844984));
#168697=CARTESIAN_POINT('Ctrl Pts',(-20.5951589428895,-19.9705363655188,
19.0469412897193));
#168698=CARTESIAN_POINT('Ctrl Pts',(-20.4745384933959,-20.1600369636971,
19.0346705631078));
#168699=CARTESIAN_POINT('Ctrl Pts',(-20.424946872753,-20.2285283032494,
19.0300002618005));
#168700=CARTESIAN_POINT('Ctrl Pts',(-20.3421887490743,-20.3295128457888,
19.0225609493452));
#168701=CARTESIAN_POINT('Ctrl Pts',(-20.3118242167303,-20.3641908420019,
19.0198954814367));
#168702=CARTESIAN_POINT('Ctrl Pts',(-20.2723344322215,-20.4064256773093,
19.0164915252927));
#168703=CARTESIAN_POINT('Ctrl Pts',(-20.2642438498836,-20.4149356198052,
19.0157972779396));
#168704=CARTESIAN_POINT('Ctrl Pts',(-20.2510482847131,-20.4285859189328,
19.0146697880743));
#168705=CARTESIAN_POINT('Ctrl Pts',(-20.2459869069728,-20.4337682225244,
19.0142384441464));
#168706=CARTESIAN_POINT('Ctrl Pts',(-20.2364228594554,-20.4434607492014,
19.0134254157127));
#168707=CARTESIAN_POINT('Ctrl Pts',(-20.2319262169406,-20.4479768254385,
19.0130439990868));
#168708=CARTESIAN_POINT('Ctrl Pts',(-20.2217842508737,-20.4580710500403,
19.0121855629858));
#168709=CARTESIAN_POINT('Ctrl Pts',(-20.2161278360035,-20.4636378732966,
19.0117080518042));
#168710=CARTESIAN_POINT('Ctrl Pts',(-20.2016527358749,-20.4777243522739,
19.0104891790842));
#168711=CARTESIAN_POINT('Ctrl Pts',(-20.1927911767316,-20.4861993498263,
19.0097458901678));
#168712=CARTESIAN_POINT('Ctrl Pts',(-20.1404571056509,-20.5353871238404,
19.0053724901324));
#168713=CARTESIAN_POINT('Ctrl Pts',(-20.0953593372162,-20.5743242650997,
19.0016676799959));
#168714=CARTESIAN_POINT('Ctrl Pts',(-20.0316930886739,-20.6247676297405,
18.9965181924037));
#168715=CARTESIAN_POINT('Ctrl Pts',(-20.014497268834,-20.6379672574055,
18.9951350650169));
#168716=CARTESIAN_POINT('Ctrl Pts',(-19.8794468682004,-20.7383748396772,
18.9843343767586));
#168717=CARTESIAN_POINT('Ctrl Pts',(-19.7530285424352,-20.81338584319,18.9745457590368));
#168718=CARTESIAN_POINT('Ctrl Pts',(-19.5428056802728,-20.9102458051805,
18.9593613002898));
#168719=CARTESIAN_POINT('Ctrl Pts',(-19.4636409328154,-20.9411004824349,
18.9538735221868));
#168720=CARTESIAN_POINT('Ctrl Pts',(-19.3742264924981,-20.9698901633591,
18.948076651573));
#168721=CARTESIAN_POINT('Ctrl Pts',(-19.3656062682177,-20.9726049098492,
18.9475218466409));
#168722=CARTESIAN_POINT('Ctrl Pts',(-19.3526781252441,-20.9765855210615,
18.9466961190504));
#168723=CARTESIAN_POINT('Ctrl Pts',(-19.3483832638059,-20.9778929786051,
18.9464228468279));
#168724=CARTESIAN_POINT('Ctrl Pts',(-19.3406711202252,-20.9802139572299,
18.9459340512265));
#168725=CARTESIAN_POINT('Ctrl Pts',(-19.3372554230306,-20.9812325149156,
18.9457182375612));
#168726=CARTESIAN_POINT('Ctrl Pts',(-19.3298331875,-20.983425421542,18.9452507443392));
#168727=CARTESIAN_POINT('Ctrl Pts',(-19.3258257556537,-20.98459654291,18.9449992540703));
#168728=CARTESIAN_POINT('Ctrl Pts',(-19.3147670694102,-20.9877928263123,
18.9443077227867));
#168729=CARTESIAN_POINT('Ctrl Pts',(-19.307708634938,-20.9897932246301,
18.9438690992699));
#168730=CARTESIAN_POINT('Ctrl Pts',(-19.2715731226257,-20.999831587648,
18.9416369955832));
#168731=CARTESIAN_POINT('Ctrl Pts',(-19.2423354437312,-21.0072844962874,
18.9398752897849));
#168732=CARTESIAN_POINT('Ctrl Pts',(-19.2027335650158,-21.0164824490094,
18.9375362327433));
#168733=CARTESIAN_POINT('Ctrl Pts',(-19.192502676619,-21.0187787109349,
18.9369361567872));
#168734=CARTESIAN_POINT('Ctrl Pts',(-19.1705246523172,-21.0235403175917,
18.9356552658465));
#168735=CARTESIAN_POINT('Ctrl Pts',(-19.1587727230442,-21.0259819678006,
18.9349753548543));
#168736=CARTESIAN_POINT('Ctrl Pts',(-19.1234977608104,-21.0329984927052,
18.9329477864644));
#168737=CARTESIAN_POINT('Ctrl Pts',(-19.0999167355877,-21.0372741391224,
18.9316099902256));
#168738=CARTESIAN_POINT('Ctrl Pts',(-18.9283590008404,-21.0653806393162,
18.9219730308797));
#168739=CARTESIAN_POINT('Ctrl Pts',(-18.7782941981129,-21.0738374330462,
18.9140271191554));
#168740=CARTESIAN_POINT('Ctrl Pts',(-18.5704646403503,-21.0634762923353,
18.9024847385498));
#168741=CARTESIAN_POINT('Ctrl Pts',(-18.5124872451802,-21.0581831131055,
18.8992105558202));
#168742=CARTESIAN_POINT('Ctrl Pts',(-18.419428987557,-21.0458021992431,
18.8938159508115));
#168743=CARTESIAN_POINT('Ctrl Pts',(-18.3841799002073,-21.040202157071,
18.8917401443556));
#168744=CARTESIAN_POINT('Ctrl Pts',(-18.3383089138505,-21.0317206023909,
18.8889896322473));
#168745=CARTESIAN_POINT('Ctrl Pts',(-18.3275430028109,-21.0296433578121,
18.8883405318056));
#168746=CARTESIAN_POINT('Ctrl Pts',(-18.3099974312121,-21.0261164093798,
18.8872766718811));
#168747=CARTESIAN_POINT('Ctrl Pts',(-18.3032078124744,-21.0247168517207,
18.8868635182677));
#168748=CARTESIAN_POINT('Ctrl Pts',(-18.2901206645844,-21.0219520905929,
18.8860642642592));
#168749=CARTESIAN_POINT('Ctrl Pts',(-18.2838222460605,-21.0205914314318,
18.8856783135041));
#168750=CARTESIAN_POINT('Ctrl Pts',(-18.2693539428215,-21.0173966089358,
18.8847887083027));
#168751=CARTESIAN_POINT('Ctrl Pts',(-18.2611885711994,-21.0155426965062,
18.8842844243636));
#168752=CARTESIAN_POINT('Ctrl Pts',(-18.2393911307814,-21.0104575144856,
18.8829321912848));
#168753=CARTESIAN_POINT('Ctrl Pts',(-18.2257799554528,-21.0071393247082,
18.8820814586356));
#168754=CARTESIAN_POINT('Ctrl Pts',(-18.1136118692846,-20.978612072223,
18.8750170282548));
#168755=CARTESIAN_POINT('Ctrl Pts',(-18.0169708302706,-20.9464678091623,
18.8685773986194));
#168756=CARTESIAN_POINT('Ctrl Pts',(-17.8305334408218,-20.8691497678742,
18.8554747869802));
#168757=CARTESIAN_POINT('Ctrl Pts',(-17.7408830926317,-20.8242798951722,
18.8488338622719));
#168758=CARTESIAN_POINT('Ctrl Pts',(-17.589756719946,-20.7347236982332,
18.8372454021194));
#168759=CARTESIAN_POINT('Ctrl Pts',(-17.5268671467347,-20.692755096443,
18.8322926809812));
#168760=CARTESIAN_POINT('Ctrl Pts',(-17.438510254664,-20.6266951421875,
18.825268033006));
#168761=CARTESIAN_POINT('Ctrl Pts',(-17.4111831235301,-20.6051948871866,
18.8230858169131));
#168762=CARTESIAN_POINT('Ctrl Pts',(-17.3787042536051,-20.5783200856179,
18.8204927089629));
#168763=CARTESIAN_POINT('Ctrl Pts',(-17.3730368862902,-20.5735803982237,
18.8200402488417));
#168764=CARTESIAN_POINT('Ctrl Pts',(-17.3642308490207,-20.5661371164649,
18.819337402556));
#168765=CARTESIAN_POINT('Ctrl Pts',(-17.3610751693034,-20.5634538676797,
18.8190855737166));
#168766=CARTESIAN_POINT('Ctrl Pts',(-17.3552161736274,-20.5584423078902,
18.8186181219436));
#168767=CARTESIAN_POINT('Ctrl Pts',(-17.3525108949523,-20.5561164488094,
18.8184023315147));
#168768=CARTESIAN_POINT('Ctrl Pts',(-17.3463808826382,-20.550819171255,
18.817913453326));
#168769=CARTESIAN_POINT('Ctrl Pts',(-17.3429598154517,-20.5478435897952,
18.8176406788191));
#168770=CARTESIAN_POINT('Ctrl Pts',(-17.3341210604825,-20.5401057848045,
18.8169360099627));
#168771=CARTESIAN_POINT('Ctrl Pts',(-17.3287180535502,-20.5353267771954,
18.8165053323724));
#168772=CARTESIAN_POINT('Ctrl Pts',(-17.2950320836536,-20.5052229696398,
18.8138198992678));
#168773=CARTESIAN_POINT('Ctrl Pts',(-17.2674082788896,-20.4791671100277,
18.8116163808876));
#168774=CARTESIAN_POINT('Ctrl Pts',(-17.2308562317907,-20.4427826482404,
18.8086742361685));
#168775=CARTESIAN_POINT('Ctrl Pts',(-17.2213066264068,-20.4330917809823,
18.8079030088112));
#168776=CARTESIAN_POINT('Ctrl Pts',(-17.2112952552922,-20.422734476272,
18.807090887949));
#168777=CARTESIAN_POINT('Ctrl Pts',(-17.2107399080521,-20.4221592878094,
18.807045826408));
#168778=CARTESIAN_POINT('Ctrl Pts',(-17.1944161843139,-20.4052331777018,
18.8057209460512));
#168779=CARTESIAN_POINT('Ctrl Pts',(-17.1789112679958,-20.3886294167988,
18.8044527961303));
#168780=CARTESIAN_POINT('Ctrl Pts',(-17.1329880829459,-20.3378368123648,
18.8006557411102));
#168781=CARTESIAN_POINT('Ctrl Pts',(-17.1034075887493,-20.3029076412833,
18.7981536164331));
#168782=CARTESIAN_POINT('Ctrl Pts',(-17.0070546926899,-20.1813520597451,
18.7897086840485));
#168783=CARTESIAN_POINT('Ctrl Pts',(-16.9458702353789,-20.0905243267209,
18.783820547421));
#168784=CARTESIAN_POINT('Ctrl Pts',(-16.8648158224065,-19.9474279256523,
18.7746761031606));
#168785=CARTESIAN_POINT('Ctrl Pts',(-16.8395383235755,-19.8984357115446,
18.7715685248052));
#168786=CARTESIAN_POINT('Ctrl Pts',(-16.8016731365264,-19.8174356950758,
18.766424420314));
#168787=CARTESIAN_POINT('Ctrl Pts',(-16.7879025051405,-19.7860086291589,
18.764427283714));
#168788=CARTESIAN_POINT('Ctrl Pts',(-16.770805923096,-19.7442593327396,
18.7617666083343));
#168789=CARTESIAN_POINT('Ctrl Pts',(-16.7667864623853,-19.7342254948354,
18.7611265985202));
#168790=CARTESIAN_POINT('Ctrl Pts',(-16.7603280058484,-19.7177384961508,
18.7600738874625));
#168791=CARTESIAN_POINT('Ctrl Pts',(-16.7578433705078,-19.7113033379144,
18.7596627275281));
#168792=CARTESIAN_POINT('Ctrl Pts',(-16.753094050289,-19.6988214706448,
18.7588646586925));
#168793=CARTESIAN_POINT('Ctrl Pts',(-16.7508254878549,-19.6927763114206,
18.7584778851739));
#168794=CARTESIAN_POINT('Ctrl Pts',(-16.7456503700919,-19.6787917384499,
18.757582507869));
#168795=CARTESIAN_POINT('Ctrl Pts',(-16.7427636652246,-19.6708451416441,
18.7570732479592));
#168796=CARTESIAN_POINT('Ctrl Pts',(-16.7351261853733,-19.6494214459058,
18.7556989424269));
#168797=CARTESIAN_POINT('Ctrl Pts',(-16.7304642018614,-19.6359133643013,
18.7548309687565));
#168798=CARTESIAN_POINT('Ctrl Pts',(-16.6889407429399,-19.5115299004638,
18.7468240931555));
#168799=CARTESIAN_POINT('Ctrl Pts',(-16.6611867852816,-19.3978459886919,
18.7393834481075));
#168800=CARTESIAN_POINT('Ctrl Pts',(-16.617554813345,-19.1217642921793,
18.7211261676592));
#168801=CARTESIAN_POINT('Ctrl Pts',(-16.6107676288211,-18.9586716078051,
18.7101695359371));
#168802=CARTESIAN_POINT('Ctrl Pts',(-16.625116472538,-18.763962999007,18.6977634339929));
#168803=CARTESIAN_POINT('Ctrl Pts',(-16.6282556713315,-18.7315714681105,
18.6957241277608));
#168804=CARTESIAN_POINT('Ctrl Pts',(-16.6330050910102,-18.6920734080976,
18.6932777762389));
#168805=CARTESIAN_POINT('Ctrl Pts',(-16.6339065251174,-18.6848879616618,
18.6928343800313));
#168806=CARTESIAN_POINT('Ctrl Pts',(-16.635377360365,-18.6736317018907,
18.6921425093426));
#168807=CARTESIAN_POINT('Ctrl Pts',(-16.6359217663822,-18.6695577594204,
18.6918926631901));
#168808=CARTESIAN_POINT('Ctrl Pts',(-16.6369614490486,-18.6619464295358,
18.6914269575609));
#168809=CARTESIAN_POINT('Ctrl Pts',(-16.637453807932,-18.6584087489876,
18.6912109424627));
#168810=CARTESIAN_POINT('Ctrl Pts',(-16.6385980423542,-18.6503369122301,
18.6907190560538));
#168811=CARTESIAN_POINT('Ctrl Pts',(-16.6392556808069,-18.6458036238921,
18.6904435137001));
#168812=CARTESIAN_POINT('Ctrl Pts',(-16.6410093635184,-18.6339851099412,
18.6897269298364));
#168813=CARTESIAN_POINT('Ctrl Pts',(-16.6421287422083,-18.6267033367755,
18.6892871742542));
#168814=CARTESIAN_POINT('Ctrl Pts',(-16.6496775325287,-18.5792479470982,
18.6864318726787));
#168815=CARTESIAN_POINT('Ctrl Pts',(-16.6572263447316,-18.5392580568182,
18.6840752747795));
#168816=CARTESIAN_POINT('Ctrl Pts',(-16.7012325912737,-18.3381313288946,
18.6723623766029));
#168817=CARTESIAN_POINT('Ctrl Pts',(-16.755311159214,-18.1814295429752,
18.6636540561542));
#168818=CARTESIAN_POINT('Ctrl Pts',(-16.8688103461087,-17.9460203983827,
18.6492830447601));
#168819=CARTESIAN_POINT('Ctrl Pts',(-16.9163963096844,-17.8623940612575,
18.6438960223989));
#168820=CARTESIAN_POINT('Ctrl Pts',(-16.981361537848,-17.7643937083535,
18.6370500809416));
#168821=CARTESIAN_POINT('Ctrl Pts',(-16.9934998848225,-17.7466744912295,
18.6357899162245));
#168822=CARTESIAN_POINT('Ctrl Pts',(-17.011118166293,-17.7217770018929,
18.6339857522627));
#168823=CARTESIAN_POINT('Ctrl Pts',(-17.0163779179723,-17.7144440144058,
18.6334501712852));
#168824=CARTESIAN_POINT('Ctrl Pts',(-17.0255236048591,-17.7018639930273,
18.6325239752543));
#168825=CARTESIAN_POINT('Ctrl Pts',(-17.0293872533033,-17.696600855899,
18.6321342264623));
#168826=CARTESIAN_POINT('Ctrl Pts',(-17.0368253580583,-17.6865661698451,
18.6313867666064));
#168827=CARTESIAN_POINT('Ctrl Pts',(-17.0403957501144,-17.6817916755942,
18.6310292166688));
#168828=CARTESIAN_POINT('Ctrl Pts',(-17.0497187927543,-17.6694336596269,
18.63009874572));
#168829=CARTESIAN_POINT('Ctrl Pts',(-17.0555024594921,-17.6618738029092,
18.6295246075421));
#168830=CARTESIAN_POINT('Ctrl Pts',(-17.075326604212,-17.6363205327975,
18.6275669241029));
#168831=CARTESIAN_POINT('Ctrl Pts',(-17.0896066152183,-17.6185157569683,
18.6261738888624));
#168832=CARTESIAN_POINT('Ctrl Pts',(-17.2175908351106,-17.4641234547488,
18.6138322323236));
#168833=CARTESIAN_POINT('Ctrl Pts',(-17.347767950318,-17.3421522553987,
18.6021595051791));
#168834=CARTESIAN_POINT('Ctrl Pts',(-17.5608059625954,-17.1877414484718,
18.5847774815365));
#168835=CARTESIAN_POINT('Ctrl Pts',(-17.6329801407193,-17.1418205527485,
18.5791489341356));
#168836=CARTESIAN_POINT('Ctrl Pts',(-17.7404724239291,-17.0822425911255,
18.5713050471948));
#168837=CARTESIAN_POINT('Ctrl Pts',(-17.7736857697627,-17.0649687893629,
18.5689513812888));
#168838=CARTESIAN_POINT('Ctrl Pts',(-17.8141293276727,-17.0452792722294,
18.5661835257967));
#168839=CARTESIAN_POINT('Ctrl Pts',(-17.8209344618584,-17.0420111742423,
18.5657210818046));
#168840=CARTESIAN_POINT('Ctrl Pts',(-17.831532257993,-17.0369912729783,
18.5650061613102));
#168841=CARTESIAN_POINT('Ctrl Pts',(-17.8353127896917,-17.0352142141969,
18.5647521621775));
#168842=CARTESIAN_POINT('Ctrl Pts',(-17.8423286386088,-17.0319416971265,
18.5642827410658));
#168843=CARTESIAN_POINT('Ctrl Pts',(-17.8455624437339,-17.0304432321504,
18.5640671387365));
#168844=CARTESIAN_POINT('Ctrl Pts',(-17.8528754370741,-17.0270769802079,
18.5635812899009));
#168845=CARTESIAN_POINT('Ctrl Pts',(-17.8569567760462,-17.0252139943197,
18.5633113405767));
#168846=CARTESIAN_POINT('Ctrl Pts',(-17.8690017601801,-17.0197620892181,
18.5625181001704));
#168847=CARTESIAN_POINT('Ctrl Pts',(-17.8769818422535,-17.0162094168027,
18.5619969822795));
#168848=CARTESIAN_POINT('Ctrl Pts',(-17.9342274191187,-16.9911475003937,
18.5582886788683));
#168849=CARTESIAN_POINT('Ctrl Pts',(-17.9842788334147,-16.9714702931428,
18.5552044604606));
#168850=CARTESIAN_POINT('Ctrl Pts',(-18.0364923719037,-16.9532067363277,
18.5520946784626));
#168851=CARTESIAN_POINT('Ctrl Pts',(-18.0379559090074,-16.9526966149244,
18.5520075976884));
#168852=CARTESIAN_POINT('Ctrl Pts',(-18.1787996364259,-16.9037783967077,
18.5436355128065));
#168853=CARTESIAN_POINT('Ctrl Pts',(-18.3228650501247,-16.8700699364164,
18.5358120090095));
#168854=CARTESIAN_POINT('Ctrl Pts',(-18.5662389656421,-16.8393956746015,
18.5223331392241));
#168855=CARTESIAN_POINT('Ctrl Pts',(-18.6639242859854,-16.8339048778165,
18.5168604198529));
#168856=CARTESIAN_POINT('Ctrl Pts',(-18.7832992610546,-16.8354631813626,
18.5099106098063));
#168857=CARTESIAN_POINT('Ctrl Pts',(-18.8049596250557,-16.8360786398982,
18.50863940879));
#168858=CARTESIAN_POINT('Ctrl Pts',(-18.8356538421519,-16.8374226157459,
18.5068221617254));
#168859=CARTESIAN_POINT('Ctrl Pts',(-18.8446987867519,-16.8378768265888,
18.5062847035758));
#168860=CARTESIAN_POINT('Ctrl Pts',(-18.8602649170903,-16.8387586800772,
18.5053562810387));
#168861=CARTESIAN_POINT('Ctrl Pts',(-18.8667875975498,-16.8391585109201,
18.5049661940694));
#168862=CARTESIAN_POINT('Ctrl Pts',(-18.8792507408218,-16.8399804241266,
18.5042187928254));
#168863=CARTESIAN_POINT('Ctrl Pts',(-18.8851914873641,-16.8403973859639,
18.5038616430946));
#168864=CARTESIAN_POINT('Ctrl Pts',(-18.9005867810982,-16.8415432333615,
18.5029337550768));
#168865=CARTESIAN_POINT('Ctrl Pts',(-18.9100382548807,-16.842310580268,
18.5023618130409));
#168866=CARTESIAN_POINT('Ctrl Pts',(-18.9420026249255,-16.845121998504,
18.5004196024337));
#168867=CARTESIAN_POINT('Ctrl Pts',(-18.9644872258126,-16.8474630956609,
18.4990400465018));
#168868=CARTESIAN_POINT('Ctrl Pts',(-19.1659646252665,-16.8717083478782,
18.48655401906));
#168869=CARTESIAN_POINT('Ctrl Pts',(-19.3414814959413,-16.916036429476,
18.4746990812069));
#168870=CARTESIAN_POINT('Ctrl Pts',(-19.5870799694235,-17.0126844155213,
18.4572659613174));
#168871=CARTESIAN_POINT('Ctrl Pts',(-19.6630624637443,-17.0479161956431,
18.4517594236141));
#168872=CARTESIAN_POINT('Ctrl Pts',(-19.7693192400267,-17.1050648387745,
18.4440621305226));
#168873=CARTESIAN_POINT('Ctrl Pts',(-19.801412629804,-17.1234251229429,
18.4417382564612));
#168874=CARTESIAN_POINT('Ctrl Pts',(-19.8394398813312,-17.1465227084929,
18.4390006679966));
#168875=CARTESIAN_POINT('Ctrl Pts',(-19.8458481765314,-17.1504619855159,
18.4385398941677));
#168876=CARTESIAN_POINT('Ctrl Pts',(-19.8557774679868,-17.156638834849,
18.4378269923529));
#168877=CARTESIAN_POINT('Ctrl Pts',(-19.8593130024129,-17.1588527533109,
18.4375733552395));
#168878=CARTESIAN_POINT('Ctrl Pts',(-19.8658576198338,-17.1629779108889,
18.437104266573));
#168879=CARTESIAN_POINT('Ctrl Pts',(-19.8688683922354,-17.1648862824385,
18.4368886368044));
#168880=CARTESIAN_POINT('Ctrl Pts',(-19.875664115456,-17.1692178360058,
18.4364023005712));
#168881=CARTESIAN_POINT('Ctrl Pts',(-19.8794461686522,-17.1716454644224,
18.4361318938939));
#168882=CARTESIAN_POINT('Ctrl Pts',(-19.8905864547267,-17.178846397086,
18.4353360617012));
#168883=CARTESIAN_POINT('Ctrl Pts',(-19.8979228908496,-17.1836534737331,
18.4348128306544));
#168884=CARTESIAN_POINT('Ctrl Pts',(-19.9507598073018,-17.2187452588739,
18.4310491803284));
#168885=CARTESIAN_POINT('Ctrl Pts',(-19.9951063287632,-17.2507391902587,
18.4279152484629));
#168886=CARTESIAN_POINT('Ctrl Pts',(-20.170748993613,-17.3881042084054,
18.4153889146402));
#168887=CARTESIAN_POINT('Ctrl Pts',(-20.2904970130694,-17.5072362487569,
18.4065304642861));
#168888=CARTESIAN_POINT('Ctrl Pts',(-20.4314208538506,-17.6855384677565,
18.3939311762484));
#168889=CARTESIAN_POINT('Ctrl Pts',(-20.4660160948721,-17.7332786000341,
18.3906172558238));
#168890=CARTESIAN_POINT('Ctrl Pts',(-20.5184690035989,-17.8124140110896,
18.3851631042797));
#168891=CARTESIAN_POINT('Ctrl Pts',(-20.5375947632265,-17.8429321234849,
18.3830687895095));
#168892=CARTESIAN_POINT('Ctrl Pts',(-20.561533971098,-17.8833889434387,
18.3802971754126));
#168893=CARTESIAN_POINT('Ctrl Pts',(-20.5670618765798,-17.8928993648179,
18.3796459830346));
#168894=CARTESIAN_POINT('Ctrl Pts',(-20.5759561220545,-17.908479606408,
18.3785795562632));
#168895=CARTESIAN_POINT('Ctrl Pts',(-20.5793672184751,-17.9145237377989,
18.3781659427359));
#168896=CARTESIAN_POINT('Ctrl Pts',(-20.585886554327,-17.9262092439177,
18.377366403494));
#168897=CARTESIAN_POINT('Ctrl Pts',(-20.5889988936711,-17.9318482522595,
18.3769806306582));
#168898=CARTESIAN_POINT('Ctrl Pts',(-20.5960893389943,-17.9448346202786,
18.3760923004983));
#168899=CARTESIAN_POINT('Ctrl Pts',(-20.6000497593598,-17.9521914678435,
18.3755891195677));
#168900=CARTESIAN_POINT('Ctrl Pts',(-20.6105051183036,-17.9718917994043,
18.3742417625404));
#168901=CARTESIAN_POINT('Ctrl Pts',(-20.6169217092727,-17.9842761933128,
18.373394834383));
#168902=CARTESIAN_POINT('Ctrl Pts',(-20.66082896707,-18.0711099103844,18.3674561459947));
#168903=CARTESIAN_POINT('Ctrl Pts',(-20.69400575322,-18.1476324499798,18.3622161288494));
#168904=CARTESIAN_POINT('Ctrl Pts',(-20.7225805841812,-18.2258896363379,
18.3568546368673));
#168905=CARTESIAN_POINT('',(-20.8509999550625,-18.9515638056372,18.8870728069919));
#168906=CARTESIAN_POINT('Ctrl Pts',(-20.7225805578636,-18.2258895642624,
18.13180632455));
#168907=CARTESIAN_POINT('Ctrl Pts',(-20.7014549938187,-18.1680335083984,
18.1356559381945));
#168908=CARTESIAN_POINT('Ctrl Pts',(-20.6778120416058,-18.1111198991202,
18.1395843440012));
#168909=CARTESIAN_POINT('Ctrl Pts',(-20.5968951827222,-17.9380659014343,
18.1519521181181));
#168910=CARTESIAN_POINT('Ctrl Pts',(-20.5314382088161,-17.826099002912,
18.1605860373068));
#168911=CARTESIAN_POINT('Ctrl Pts',(-20.4404277236397,-17.6987934812837,
18.1708507178815));
#168912=CARTESIAN_POINT('Ctrl Pts',(-20.4242591457825,-17.6770701000627,
18.1726185562031));
#168913=CARTESIAN_POINT('Ctrl Pts',(-20.3725006369513,-17.610245633393,
18.1780953939198));
#168914=CARTESIAN_POINT('Ctrl Pts',(-20.335485787003,-17.5662750447385,
18.1817561699393));
#168915=CARTESIAN_POINT('Ctrl Pts',(-20.2907365793565,-17.5173087400105,
18.185849353701));
#168916=CARTESIAN_POINT('Ctrl Pts',(-20.2847072997032,-17.5107940237516,
18.1863942725033));
#168917=CARTESIAN_POINT('Ctrl Pts',(-20.2755484278858,-17.5010217627692,
18.1872119191199));
#168918=CARTESIAN_POINT('Ctrl Pts',(-20.2724491807455,-17.4977360901224,
18.1874868754641));
#168919=CARTESIAN_POINT('Ctrl Pts',(-20.2668840417111,-17.4918738982177,
18.1879774801173));
#168920=CARTESIAN_POINT('Ctrl Pts',(-20.2644221416631,-17.4892936769958,
18.1881934280994));
#168921=CARTESIAN_POINT('Ctrl Pts',(-20.2590780218465,-17.4837209772744,
18.1886598439083));
#168922=CARTESIAN_POINT('Ctrl Pts',(-20.2561935187446,-17.480730767851,
18.1889101298111));
#168923=CARTESIAN_POINT('Ctrl Pts',(-20.2481155729387,-17.4724059812058,
18.1896070398517));
#168924=CARTESIAN_POINT('Ctrl Pts',(-20.2429027058825,-17.467090219379,
18.1900521765677));
#168925=CARTESIAN_POINT('Ctrl Pts',(-20.2125449124321,-17.4364581461821,
18.1926188135647));
#168926=CARTESIAN_POINT('Ctrl Pts',(-20.1867895801381,-17.4117516615915,
18.1946950947449));
#168927=CARTESIAN_POINT('Ctrl Pts',(-20.1021479413093,-17.3345701398256,
18.2012497117177));
#168928=CARTESIAN_POINT('Ctrl Pts',(-20.0409471990332,-17.2847270473925,
18.2055909871369));
#168929=CARTESIAN_POINT('Ctrl Pts',(-19.903373021049,-17.1849253647089,
18.2148602753393));
#168930=CARTESIAN_POINT('Ctrl Pts',(-19.8262683337281,-17.1362533788287,
18.2197672875293));
#168931=CARTESIAN_POINT('Ctrl Pts',(-19.6529455460105,-17.0418903602357,
18.230613276237));
#168932=CARTESIAN_POINT('Ctrl Pts',(-19.5559411864842,-16.998186246701,
18.2365761377173));
#168933=CARTESIAN_POINT('Ctrl Pts',(-19.442814703661,-16.9571391848231,
18.2436279543692));
#168934=CARTESIAN_POINT('Ctrl Pts',(-19.4295078667641,-16.9524608658553,
18.2444587326609));
#168935=CARTESIAN_POINT('Ctrl Pts',(-19.4082025585544,-16.9452089078474,
18.2457913443706));
#168936=CARTESIAN_POINT('Ctrl Pts',(-19.4002336548818,-16.9425492562635,
18.2462903324053));
#168937=CARTESIAN_POINT('Ctrl Pts',(-19.3861206984003,-16.937932182544,
18.2471750914626));
#168938=CARTESIAN_POINT('Ctrl Pts',(-19.3799831034924,-16.9359552566532,
18.2475602140492));
#168939=CARTESIAN_POINT('Ctrl Pts',(-19.3672398197472,-16.931914797986,
18.2483605946615));
#168940=CARTESIAN_POINT('Ctrl Pts',(-19.3606328603838,-16.9298555567845,
18.2487759883668));
#168941=CARTESIAN_POINT('Ctrl Pts',(-19.3435841033661,-16.9246334186211,
18.2498490264013));
#168942=CARTESIAN_POINT('Ctrl Pts',(-19.3331278345741,-16.9215188094375,
18.2505082421391));
#168943=CARTESIAN_POINT('Ctrl Pts',(-19.2888353712428,-16.9086973267133,
18.253305627886));
#168944=CARTESIAN_POINT('Ctrl Pts',(-19.2547854885508,-16.8997548038335,
18.2554684570319));
#168945=CARTESIAN_POINT('Ctrl Pts',(-19.1649573471851,-16.8785426694681,
18.2612098529141));
#168946=CARTESIAN_POINT('Ctrl Pts',(-19.1088807585081,-16.8676744384256,
18.2648301037279));
#168947=CARTESIAN_POINT('Ctrl Pts',(-18.9020629067177,-16.8362070632004,
18.2782981352708));
#168948=CARTESIAN_POINT('Ctrl Pts',(-18.7496651390731,-16.8296021315434,
18.2884844088056));
#168949=CARTESIAN_POINT('Ctrl Pts',(-18.5754010006632,-16.840828870881,
18.2998902146444));
#168950=CARTESIAN_POINT('Ctrl Pts',(-18.5529288208721,-16.8426374286151,
18.3013554564997));
#168951=CARTESIAN_POINT('Ctrl Pts',(-18.4793873770739,-16.849739983946,
18.3061241724256));
#168952=CARTESIAN_POINT('Ctrl Pts',(-18.4284771731252,-16.8565331066087,
18.3093838584664));
#168953=CARTESIAN_POINT('Ctrl Pts',(-18.3700974592668,-16.8664962344705,
18.3130366263678));
#168954=CARTESIAN_POINT('Ctrl Pts',(-18.3623420350525,-16.8678643574166,
18.3135201223377));
#168955=CARTESIAN_POINT('Ctrl Pts',(-18.3499884060835,-16.8701147932966,
18.3142872879271));
#168956=CARTESIAN_POINT('Ctrl Pts',(-18.3453852680358,-16.8709691234335,
18.3145724800176));
#168957=CARTESIAN_POINT('Ctrl Pts',(-18.3372545430383,-16.8725060828346,
18.3150750056348));
#168958=CARTESIAN_POINT('Ctrl Pts',(-18.3337258118384,-16.8731824312398,
18.3152926927288));
#168959=CARTESIAN_POINT('Ctrl Pts',(-18.3262688272122,-16.8746313957052,
18.3157518340066));
#168960=CARTESIAN_POINT('Ctrl Pts',(-18.3223410457445,-16.8754061703439,
18.3159931635101));
#168961=CARTESIAN_POINT('Ctrl Pts',(-18.3117872920027,-16.8775190715405,
18.3166402846104));
#168962=CARTESIAN_POINT('Ctrl Pts',(-18.3051654272027,-16.8788778122531,
18.3170449155871));
#168963=CARTESIAN_POINT('Ctrl Pts',(-18.2728534276812,-16.8856693564059,
18.3190130075689));
#168964=CARTESIAN_POINT('Ctrl Pts',(-18.2472581438509,-16.8915483509178,
18.3205523838813));
#168965=CARTESIAN_POINT('Ctrl Pts',(-18.1742477755915,-16.90975466547,18.3249042227588));
#168966=CARTESIAN_POINT('Ctrl Pts',(-18.1271404442043,-16.9232539168036,
18.3276643906846));
#168967=CARTESIAN_POINT('Ctrl Pts',(-17.9886552848986,-16.9681949688881,
18.3357480313417));
#168968=CARTESIAN_POINT('Ctrl Pts',(-17.8989149530236,-17.0042691253555,
18.3409499996545));
#168969=CARTESIAN_POINT('Ctrl Pts',(-17.6849954408331,-17.1077741520989,
18.3538813167751));
#168970=CARTESIAN_POINT('Ctrl Pts',(-17.5645156751023,-17.1817236301917,
18.3616604519692));
#168971=CARTESIAN_POINT('Ctrl Pts',(-17.4409213177332,-17.2757421061207,
18.3707579533706));
#168972=CARTESIAN_POINT('Ctrl Pts',(-17.4296415644068,-17.284504254298,
18.3715990630707));
#168973=CARTESIAN_POINT('Ctrl Pts',(-17.4118290307724,-17.2986324133433,
18.3729451247101));
#168974=CARTESIAN_POINT('Ctrl Pts',(-17.4052381145669,-17.3039246688532,
18.373447139033));
#168975=CARTESIAN_POINT('Ctrl Pts',(-17.3936690413186,-17.3133287066519,
18.3743354160077));
#168976=CARTESIAN_POINT('Ctrl Pts',(-17.388677641671,-17.3174240803199,
18.3747210132844));
#168977=CARTESIAN_POINT('Ctrl Pts',(-17.3783916763289,-17.3259425997679,
18.37552056087));
#168978=CARTESIAN_POINT('Ctrl Pts',(-17.3730998476463,-17.3303689169152,
18.3759346378823));
#168979=CARTESIAN_POINT('Ctrl Pts',(-17.3595700160993,-17.3417987292534,
18.3770004261615));
#168980=CARTESIAN_POINT('Ctrl Pts',(-17.3513639371501,-17.3488395514256,
18.3776536684712));
#168981=CARTESIAN_POINT('Ctrl Pts',(-17.3173224481639,-17.3785029531639,
18.3803925052116));
#168982=CARTESIAN_POINT('Ctrl Pts',(-17.2919866618019,-17.4016885610366,
18.3825014902353));
#168983=CARTESIAN_POINT('Ctrl Pts',(-17.2274363561534,-17.4637123686315,
18.3880659656966));
#168984=CARTESIAN_POINT('Ctrl Pts',(-17.1891587191538,-17.5034839733387,
18.3915600140813));
#168985=CARTESIAN_POINT('Ctrl Pts',(-17.0797163025748,-17.6264752538766,
18.4021429232626));
#168986=CARTESIAN_POINT('Ctrl Pts',(-17.01340853863,-17.7137625578543,18.4093801300626));
#168987=CARTESIAN_POINT('Ctrl Pts',(-16.9253080517563,-17.8505644145418,
18.4201285403013));
#168988=CARTESIAN_POINT('Ctrl Pts',(-16.8981645098223,-17.8964265525134,
18.423639715754));
#168989=CARTESIAN_POINT('Ctrl Pts',(-16.8669008644352,-17.954111221494,
18.427909920835));
#168990=CARTESIAN_POINT('Ctrl Pts',(-16.8611173129325,-17.9650087916164,
18.4287103743481));
#168991=CARTESIAN_POINT('Ctrl Pts',(-16.8307021557992,-18.0235482119487,
18.4329747682623));
#168992=CARTESIAN_POINT('Ctrl Pts',(-16.8077901522222,-18.072067002497,
18.4363847848929));
#168993=CARTESIAN_POINT('Ctrl Pts',(-16.7833144611587,-18.1294482757529,
18.4402332104567));
#168994=CARTESIAN_POINT('Ctrl Pts',(-16.7799346250494,-18.137510020333,
18.4407697408754));
#168995=CARTESIAN_POINT('Ctrl Pts',(-16.7748952826621,-18.1497420325298,
18.4415772919435));
#168996=CARTESIAN_POINT('Ctrl Pts',(-16.7731989912835,-18.1538969083261,
18.4418504618232));
#168997=CARTESIAN_POINT('Ctrl Pts',(-16.7701792125227,-18.1613612593019,
18.4423391479487));
#168998=CARTESIAN_POINT('Ctrl Pts',(-16.7688508649702,-18.1646686966084,
18.4425549539098));
#168999=CARTESIAN_POINT('Ctrl Pts',(-16.7659841878458,-18.1718588561873,
18.4430225146984));
#169000=CARTESIAN_POINT('Ctrl Pts',(-16.7644489974607,-18.175742767991,
18.4432740797828));
#169001=CARTESIAN_POINT('Ctrl Pts',(-16.7601728693944,-18.1866553893398,
18.4439781737629));
#169002=CARTESIAN_POINT('Ctrl Pts',(-16.7574579633875,-18.1936943255065,
18.4444291651366));
#169003=CARTESIAN_POINT('Ctrl Pts',(-16.7415285455325,-18.2356613359817,
18.4471000682885));
#169004=CARTESIAN_POINT('Ctrl Pts',(-16.7292016041059,-18.2709219166159,
18.4492703570656));
#169005=CARTESIAN_POINT('Ctrl Pts',(-16.6918543298198,-18.3875728993103,
18.4562669189845));
#169006=CARTESIAN_POINT('Ctrl Pts',(-16.6708078754535,-18.470152062287,
18.4609339761303));
#169007=CARTESIAN_POINT('Ctrl Pts',(-16.6212760910681,-18.7287702646486,
18.4752677833373));
#169008=CARTESIAN_POINT('Ctrl Pts',(-16.6099881174692,-18.9072697929849,
18.4848334076854));
#169009=CARTESIAN_POINT('Ctrl Pts',(-16.6226185942617,-19.1078098802962,
18.496511988687));
#169010=CARTESIAN_POINT('Ctrl Pts',(-16.6244177980262,-19.1305246007929,
18.4978470478919));
#169011=CARTESIAN_POINT('Ctrl Pts',(-16.6274872989933,-19.1626744502725,
18.4997557511401));
#169012=CARTESIAN_POINT('Ctrl Pts',(-16.6284551712544,-19.1721373506553,
18.5003199016387));
#169013=CARTESIAN_POINT('Ctrl Pts',(-16.6301332275919,-19.1875188617696,
18.5012408416864));
#169014=CARTESIAN_POINT('Ctrl Pts',(-16.6308047001797,-19.1934416285285,
18.5015964080893));
#169015=CARTESIAN_POINT('Ctrl Pts',(-16.6322641807379,-19.2058467804165,
18.5023431651883));
#169016=CARTESIAN_POINT('Ctrl Pts',(-16.6330571853879,-19.212328504286,
18.5027345099705));
#169017=CARTESIAN_POINT('Ctrl Pts',(-16.6350181931231,-19.2277642331831,
18.5036692839637));
#169018=CARTESIAN_POINT('Ctrl Pts',(-16.6362135141718,-19.2367145831018,
18.504213570953));
#169019=CARTESIAN_POINT('Ctrl Pts',(-16.6404498328217,-19.2669593542716,
18.5060606148373));
#169020=CARTESIAN_POINT('Ctrl Pts',(-16.6437580302272,-19.288214442803,
18.5073717834588));
#169021=CARTESIAN_POINT('Ctrl Pts',(-16.6777802826256,-19.4868385184168,
18.5197515419801));
#169022=CARTESIAN_POINT('Ctrl Pts',(-16.7306709314759,-19.6596290421803,
18.5315691562101));
#169023=CARTESIAN_POINT('Ctrl Pts',(-16.8541184655078,-19.9328720739976,
18.5513774986948));
#169024=CARTESIAN_POINT('Ctrl Pts',(-16.9126820524977,-20.037758815324,
18.5592673568977));
#169025=CARTESIAN_POINT('Ctrl Pts',(-16.9851454801079,-20.1450160974773,
18.5672622957592));
#169026=CARTESIAN_POINT('Ctrl Pts',(-16.9905255044399,-20.1528647849307,
18.5678468110743));
#169027=CARTESIAN_POINT('Ctrl Pts',(-16.9985758131628,-20.1644408887967,
18.5687078162743));
#169028=CARTESIAN_POINT('Ctrl Pts',(-17.00120549438,-20.1681962092081,18.5689869552935));
#169029=CARTESIAN_POINT('Ctrl Pts',(-17.0059058651723,-20.1748623885648,
18.5694821102408));
#169030=CARTESIAN_POINT('Ctrl Pts',(-17.0079717397612,-20.1777765725071,
18.5696984490793));
#169031=CARTESIAN_POINT('Ctrl Pts',(-17.0124290475295,-20.1840305710991,
18.5701624510054));
#169032=CARTESIAN_POINT('Ctrl Pts',(-17.0148228206061,-20.187368649037,
18.5704099494688));
#169033=CARTESIAN_POINT('Ctrl Pts',(-17.0214568979823,-20.1965631364438,
18.5710912782805));
#169034=CARTESIAN_POINT('Ctrl Pts',(-17.0257175581805,-20.2024048861329,
18.5715237272842));
#169035=CARTESIAN_POINT('Ctrl Pts',(-17.0492173292415,-20.2342808840726,
18.5738817153347));
#169036=CARTESIAN_POINT('Ctrl Pts',(-17.0690228394063,-20.2598945776802,
18.5757702005519));
#169037=CARTESIAN_POINT('Ctrl Pts',(-17.1919348780031,-20.4115323205803,
18.5869796760874));
#169038=CARTESIAN_POINT('Ctrl Pts',(-17.3087208292305,-20.5257822670265,
18.5955854718404));
#169039=CARTESIAN_POINT('Ctrl Pts',(-17.5298999304642,-20.6971376954425,
18.610902358248));
#169040=CARTESIAN_POINT('Ctrl Pts',(-17.6281001113012,-20.7609617786794,
18.6174301598351));
#169041=CARTESIAN_POINT('Ctrl Pts',(-17.7436186511363,-20.8231058718173,
18.6251150119545));
#169042=CARTESIAN_POINT('Ctrl Pts',(-17.7562461383815,-20.829735277134,
18.6259548894507));
#169043=CARTESIAN_POINT('Ctrl Pts',(-17.7764572901219,-20.8400869427208,
18.6272993475603));
#169044=CARTESIAN_POINT('Ctrl Pts',(-17.7839980528673,-20.8438923441368,
18.6278010016303));
#169045=CARTESIAN_POINT('Ctrl Pts',(-17.7973418336955,-20.8505263108383,
18.6286888591268));
#169046=CARTESIAN_POINT('Ctrl Pts',(-17.8031354274767,-20.8533736664966,
18.6290743991974));
#169047=CARTESIAN_POINT('Ctrl Pts',(-17.8151496499936,-20.8592101785023,
18.6298740424715));
#169048=CARTESIAN_POINT('Ctrl Pts',(-17.821372046916,-20.8621954999907,
18.6302882734354));
#169049=CARTESIAN_POINT('Ctrl Pts',(-17.8373906645247,-20.8697846228885,
18.6313549100218));
#169050=CARTESIAN_POINT('Ctrl Pts',(-17.8472077081316,-20.8743437737609,
18.6320088513913));
#169051=CARTESIAN_POINT('Ctrl Pts',(-17.8884051872439,-20.8930936385064,
18.6347544773383));
#169052=CARTESIAN_POINT('Ctrl Pts',(-17.9200931354962,-20.9065921564061,
18.6368696977604));
#169053=CARTESIAN_POINT('Ctrl Pts',(-18.0035804676893,-20.9397740837947,
18.6424545636297));
#169054=CARTESIAN_POINT('Ctrl Pts',(-18.055845678762,-20.9582064660818,
18.6459631202118));
#169055=CARTESIAN_POINT('Ctrl Pts',(-18.213522134828,-21.0069484979291,
18.6565738782987));
#169056=CARTESIAN_POINT('Ctrl Pts',(-18.3206243946559,-21.031141093652,
18.6638243294742));
#169057=CARTESIAN_POINT('Ctrl Pts',(-18.4914030110207,-21.0559958421014,
18.6752237102989));
#169058=CARTESIAN_POINT('Ctrl Pts',(-18.554073482309,-21.0622793377801,
18.6793704933246));
#169059=CARTESIAN_POINT('Ctrl Pts',(-18.6249919884791,-21.0662070382063,
18.6839676911707));
#169060=CARTESIAN_POINT('Ctrl Pts',(-18.6330535776426,-21.0666072849378,
18.6844888706592));
#169061=CARTESIAN_POINT('Ctrl Pts',(-18.6891859357658,-21.0690724469979,
18.6881072421441));
#169062=CARTESIAN_POINT('Ctrl Pts',(-18.7373167833852,-21.069544292762,
18.6911561306833));
#169063=CARTESIAN_POINT('Ctrl Pts',(-18.7931633851969,-21.0681872793371,
18.6946006466039));
#169064=CARTESIAN_POINT('Ctrl Pts',(-18.8009001333698,-21.0679568246359,
18.6950757527208));
#169065=CARTESIAN_POINT('Ctrl Pts',(-18.813274915212,-21.0675202759734,
18.6958321571785));
#169066=CARTESIAN_POINT('Ctrl Pts',(-18.8179137527612,-21.0673413514798,
18.6961149132475));
#169067=CARTESIAN_POINT('Ctrl Pts',(-18.8261364253347,-21.0669971039327,
18.6966146704961));
#169068=CARTESIAN_POINT('Ctrl Pts',(-18.829720472994,-21.0668379281398,
18.6968320120634));
#169069=CARTESIAN_POINT('Ctrl Pts',(-18.837324939827,-21.0664808249313,
18.6972921050877));
#169070=CARTESIAN_POINT('Ctrl Pts',(-18.8413451955132,-21.0662805423629,
18.6975347232917));
#169071=CARTESIAN_POINT('Ctrl Pts',(-18.852212987385,-21.0657080489349,
18.6981889670667));
#169072=CARTESIAN_POINT('Ctrl Pts',(-18.8590593945063,-21.0653140271393,
18.6985993874125));
#169073=CARTESIAN_POINT('Ctrl Pts',(-18.8932695928021,-21.0631783434983,
18.7006420411886));
#169074=CARTESIAN_POINT('Ctrl Pts',(-18.9206010225113,-21.0609383635452,
18.7022479382413));
#169075=CARTESIAN_POINT('Ctrl Pts',(-18.9998397304387,-21.0528916237394,
18.7068478344047));
#169076=CARTESIAN_POINT('Ctrl Pts',(-19.0515874262013,-21.0456941857535,
18.7097821218539));
#169077=CARTESIAN_POINT('Ctrl Pts',(-19.2434591622088,-21.0117285807831,
18.7205711117203));
#169078=CARTESIAN_POINT('Ctrl Pts',(-19.3810286281969,-20.9727391869252,
18.7281483031524));
#169079=CARTESIAN_POINT('Ctrl Pts',(-19.5986152830153,-20.8865500668099,
18.7410970678788));
#169080=CARTESIAN_POINT('Ctrl Pts',(-19.681315743512,-20.8474243523152,
18.7462633657484));
#169081=CARTESIAN_POINT('Ctrl Pts',(-19.7742999114314,-20.7958244878542,
18.7524977771358));
#169082=CARTESIAN_POINT('Ctrl Pts',(-19.7872987516286,-20.7884297891322,
18.7533793034606));
#169083=CARTESIAN_POINT('Ctrl Pts',(-19.8070974068586,-20.776887494625,
18.7547378239759));
#169084=CARTESIAN_POINT('Ctrl Pts',(-19.8139541451335,-20.7728381186709,
18.7552112631254));
#169085=CARTESIAN_POINT('Ctrl Pts',(-19.8261168622928,-20.7655623288055,
18.7560564085619));
#169086=CARTESIAN_POINT('Ctrl Pts',(-19.8314318250461,-20.7623510569701,
18.7564275586831));
#169087=CARTESIAN_POINT('Ctrl Pts',(-19.8427245918092,-20.7554600228029,
18.7572200952087));
#169088=CARTESIAN_POINT('Ctrl Pts',(-19.8486983646158,-20.7517738270142,
18.7576417152163));
#169089=CARTESIAN_POINT('Ctrl Pts',(-19.8609114982971,-20.7441534202578,
18.7585086321117));
#169090=CARTESIAN_POINT('Ctrl Pts',(-19.867148845742,-20.7402161776401,
18.758954037484));
#169091=CARTESIAN_POINT('Ctrl Pts',(-19.8826137461638,-20.7303407633873,
18.7600650822019));
#169092=CARTESIAN_POINT('Ctrl Pts',(-19.8918158673302,-20.7243633427829,
18.7607321761089));
#169093=CARTESIAN_POINT('Ctrl Pts',(-20.0261796544709,-20.6355917126041,
18.7705618694351));
#169094=CARTESIAN_POINT('Ctrl Pts',(-20.1422134237702,-20.5398061363553,
18.7802400241385));
#169095=CARTESIAN_POINT('Ctrl Pts',(-20.3517752295694,-20.3256375691789,
18.7999877219203));
#169096=CARTESIAN_POINT('Ctrl Pts',(-20.4447938226567,-20.2078931310709,
18.8099925747814));
#169097=CARTESIAN_POINT('Ctrl Pts',(-20.5330045107872,-20.0680280605751,
18.8203082801053));
#169098=CARTESIAN_POINT('Ctrl Pts',(-20.5412380994583,-20.0546451591922,
18.8212804206672));
#169099=CARTESIAN_POINT('Ctrl Pts',(-20.5523029246649,-20.0362034124847,
18.822598444156));
#169100=CARTESIAN_POINT('Ctrl Pts',(-20.5552632834292,-20.0312231556703,
18.8229522502487));
#169101=CARTESIAN_POINT('Ctrl Pts',(-20.5599344129934,-20.0232908845442,
18.8235123170366));
#169102=CARTESIAN_POINT('Ctrl Pts',(-20.56165853141,-20.0203468223416,18.823719433486));
#169103=CARTESIAN_POINT('Ctrl Pts',(-20.5652041562149,-20.0142586977605,
18.8241461642087));
#169104=CARTESIAN_POINT('Ctrl Pts',(-20.5670246862172,-20.0111141121592,
18.8243657098303));
#169105=CARTESIAN_POINT('Ctrl Pts',(-20.5713425418894,-20.0036114363162,
18.8248874981458));
#169106=CARTESIAN_POINT('Ctrl Pts',(-20.5738324899966,-19.9992490817204,
18.8251892650863));
#169107=CARTESIAN_POINT('Ctrl Pts',(-20.5821739629807,-19.9845133642999,
18.8262032984603));
#169108=CARTESIAN_POINT('Ctrl Pts',(-20.587953592802,-19.9740992786041,
18.826911096927));
#169109=CARTESIAN_POINT('Ctrl Pts',(-20.6534232358866,-19.8537494480221,
18.8349959405946));
#169110=CARTESIAN_POINT('Ctrl Pts',(-20.7033526973828,-19.7387633066903,
18.8418238728466));
#169111=CARTESIAN_POINT('Ctrl Pts',(-20.7942050477999,-19.4655590440802,
18.8574732205239));
#169112=CARTESIAN_POINT('Ctrl Pts',(-20.8275799265213,-19.3057012584407,
18.8662583302302));
#169113=CARTESIAN_POINT('Ctrl Pts',(-20.8447697715777,-19.1165532345429,
18.8772499428655));
#169114=CARTESIAN_POINT('Ctrl Pts',(-20.846707235207,-19.0894584832142,
18.8788369536102));
#169115=CARTESIAN_POINT('Ctrl Pts',(-20.8486554031477,-19.0521296886354,
18.8810434997841));
#169116=CARTESIAN_POINT('Ctrl Pts',(-20.8491140970807,-19.0419209618802,
18.8816490081777));
#169117=CARTESIAN_POINT('Ctrl Pts',(-20.8497282756523,-19.0256205847214,
18.8826192609571));
#169118=CARTESIAN_POINT('Ctrl Pts',(-20.849931406149,-19.0195308090262,
18.8829825085533));
#169119=CARTESIAN_POINT('Ctrl Pts',(-20.8502862993211,-19.0073076836303,
18.8837131702452));
#169120=CARTESIAN_POINT('Ctrl Pts',(-20.8504376956036,-19.0011743831896,
18.8840805922278));
#169121=CARTESIAN_POINT('Ctrl Pts',(-20.8507174561178,-18.9874168814135,
18.8849065617177));
#169122=CARTESIAN_POINT('Ctrl Pts',(-20.8508312920819,-18.9797924991866,
18.8853655601581));
#169123=CARTESIAN_POINT('Ctrl Pts',(-20.8509693632245,-18.965299885361,
18.8862404589823));
#169124=CARTESIAN_POINT('Ctrl Pts',(-20.8510013701741,-18.9584318247995,
18.8866561084519));
#169125=CARTESIAN_POINT('Ctrl Pts',(-20.8509999550625,-18.9515638056372,
18.8870728069919));
#169126=CARTESIAN_POINT('Ctrl Pts',(-20.8509999552294,-18.9515646165639,
18.8870727577911));
#169127=CARTESIAN_POINT('Ctrl Pts',(-20.8509977754035,-18.9409654736441,
18.8877158320748));
#169128=CARTESIAN_POINT('Ctrl Pts',(-20.8509159958824,-18.9303666120166,
18.8883613944822));
#169129=CARTESIAN_POINT('Ctrl Pts',(-20.8504276848002,-18.8982971073801,
18.8903224437704));
#169130=CARTESIAN_POINT('Ctrl Pts',(-20.8497740635919,-18.8768321572957,
18.8916455393117));
#169131=CARTESIAN_POINT('Ctrl Pts',(-20.8411283389369,-18.6875938653183,
18.9034051797753));
#169132=CARTESIAN_POINT('Ctrl Pts',(-20.8135225495725,-18.5213410133495,
18.9144672333324));
#169133=CARTESIAN_POINT('Ctrl Pts',(-20.7534085349207,-18.3148990616014,
18.9286689878955));
#169134=CARTESIAN_POINT('Ctrl Pts',(-20.7387334245607,-18.2701270183631,
18.931773307545));
#169135=CARTESIAN_POINT('Ctrl Pts',(-20.7225805608153,-18.2258895723463,
18.9348455085272));
#169136=CARTESIAN_POINT('Origin',(-18.734,-18.952,0.));
#169137=CARTESIAN_POINT('',(-20.7225805743325,-18.2258896093654,19.9537493095993));
#169138=CARTESIAN_POINT('',(-20.7225805414791,-18.2258895193907,19.7345260867578));
#169139=CARTESIAN_POINT('',(-20.7225805737622,-18.2258896078036,0.));
#169140=CARTESIAN_POINT('',(-20.8479141116672,-18.9511715446921,19.9109957148815));
#169141=CARTESIAN_POINT('Ctrl Pts',(-20.7225805743325,-18.2258896093654,
19.9537493095993));
#169142=CARTESIAN_POINT('Ctrl Pts',(-20.7405652798718,-18.2751438777686,
19.9507625960589));
#169143=CARTESIAN_POINT('Ctrl Pts',(-20.7567161784059,-18.3250557419143,
19.9478476276529));
#169144=CARTESIAN_POINT('Ctrl Pts',(-20.8240164173824,-18.5628627648768,
19.934264720273));
#169145=CARTESIAN_POINT('Ctrl Pts',(-20.8509329970543,-18.7565969413757,
19.9239834015846));
#169146=CARTESIAN_POINT('Ctrl Pts',(-20.8509998750795,-18.9512727356193,
19.9127740399324));
#169147=CARTESIAN_POINT('Ctrl Pts',(-20.7202230294519,-18.2267290932703,
19.1554367770419));
#169148=CARTESIAN_POINT('Ctrl Pts',(-20.6328469384039,-17.9823750760586,
19.1710019356974));
#169149=CARTESIAN_POINT('Ctrl Pts',(-20.1480308738017,-17.1326717534008,
19.2289590299134));
#169150=CARTESIAN_POINT('Ctrl Pts',(-18.3741968410994,-16.4747290082863,
19.3293080596899));
#169151=CARTESIAN_POINT('Ctrl Pts',(-16.456252502104,-17.9136376975394,
19.4564838663714));
#169152=CARTESIAN_POINT('Ctrl Pts',(-16.6280001175491,-20.3051793956671,
19.5836596730528));
#169153=CARTESIAN_POINT('Ctrl Pts',(-18.7318719157577,-21.4552629005109,
19.7108354797342));
#169154=CARTESIAN_POINT('Ctrl Pts',(-20.5383021339267,-20.4717616627176,
19.8199301623757));
#169155=CARTESIAN_POINT('Ctrl Pts',(-20.8463943782946,-19.3568003242117,
19.8866329094569));
#169156=CARTESIAN_POINT('Ctrl Pts',(-20.847823891442,-18.9511685861152,
19.9109437209775));
#169157=CARTESIAN_POINT('Ctrl Pts',(-20.7225805608153,-18.2258895723463,
18.9348455085272));
#169158=CARTESIAN_POINT('Ctrl Pts',(-20.7101483133892,-18.191841685665,
18.9372100652618));
#169159=CARTESIAN_POINT('Ctrl Pts',(-20.6968406754583,-18.1581104763876,
18.9395554959463));
#169160=CARTESIAN_POINT('Ctrl Pts',(-20.6682555312599,-18.0907769770335,
18.9442220241356));
#169161=CARTESIAN_POINT('Ctrl Pts',(-20.6529555715504,-18.0572042398701,
18.946540783944));
#169162=CARTESIAN_POINT('Ctrl Pts',(-20.6334898971761,-18.0172895412496,
18.9492731725517));
#169163=CARTESIAN_POINT('Ctrl Pts',(-20.6301587436143,-18.0105503018847,
18.9497336570361));
#169164=CARTESIAN_POINT('Ctrl Pts',(-20.624923832368,-18.0001000826112,
18.9504462090837));
#169165=CARTESIAN_POINT('Ctrl Pts',(-20.6230449261506,-17.9963768210117,
18.9506997834402));
#169166=CARTESIAN_POINT('Ctrl Pts',(-20.6195395988019,-17.9894813617797,
18.9511688146376));
#169167=CARTESIAN_POINT('Ctrl Pts',(-20.6179161827287,-17.9863077486529,
18.9513844493235));
#169168=CARTESIAN_POINT('Ctrl Pts',(-20.6142273513526,-17.9791411633206,
18.951870870775));
#169169=CARTESIAN_POINT('Ctrl Pts',(-20.6121572347693,-17.975150671178,
18.9521413572984));
#169170=CARTESIAN_POINT('Ctrl Pts',(-20.6060078757759,-17.9633885748988,
18.9529376423619));
#169171=CARTESIAN_POINT('Ctrl Pts',(-20.601892937943,-17.9556356011869,
18.953461242705));
#169172=CARTESIAN_POINT('Ctrl Pts',(-20.5717300485923,-17.899649204765,
18.9572347038645));
#169173=CARTESIAN_POINT('Ctrl Pts',(-20.5438632214111,-17.852413648208,
18.960377446766));
#169174=CARTESIAN_POINT('Ctrl Pts',(-20.4242375867613,-17.6665375375298,
18.9727934453743));
#169175=CARTESIAN_POINT('Ctrl Pts',(-20.3181325105313,-17.5378400653005,
18.9815481062807));
#169176=CARTESIAN_POINT('Ctrl Pts',(-20.154583850435,-17.3812508164102,
18.9940889063644));
#169177=CARTESIAN_POINT('Ctrl Pts',(-20.1093578780004,-17.3415027549366,
18.997470164347));
#169178=CARTESIAN_POINT('Ctrl Pts',(-20.0340386896833,-17.2807953691487,
19.003025047076));
#169179=CARTESIAN_POINT('Ctrl Pts',(-20.0049868156137,-17.2585957980946,
19.0051505037588));
#169180=CARTESIAN_POINT('Ctrl Pts',(-19.9687427476027,-17.2323586408162,
19.0077883404947));
#169181=CARTESIAN_POINT('Ctrl Pts',(-19.9620817909277,-17.2275954161152,
19.0082725606268));
#169182=CARTESIAN_POINT('Ctrl Pts',(-19.9491828911,-17.2184841053645,19.0092092622059));
#169183=CARTESIAN_POINT('Ctrl Pts',(-19.9429488194956,-17.2141307398694,
19.0096615327218));
#169184=CARTESIAN_POINT('Ctrl Pts',(-19.9366515643159,-17.2097835331961,
19.0101179815018));
#169185=CARTESIAN_POINT('Ctrl Pts',(-19.9366116357795,-17.2097559712136,
19.0101208756562));
#169186=CARTESIAN_POINT('Ctrl Pts',(-19.9365301503012,-17.2096997273242,
19.0101267819639));
#169187=CARTESIAN_POINT('Ctrl Pts',(-19.9364885933154,-17.2096710455554,
19.0101297941191));
#169188=CARTESIAN_POINT('Ctrl Pts',(-19.9364037426463,-17.209612487867,
19.0101359442734));
#169189=CARTESIAN_POINT('Ctrl Pts',(-19.9363604488869,-17.2095826120819,
19.0101390822766));
#169190=CARTESIAN_POINT('Ctrl Pts',(-19.9362720061143,-17.20952158512,19.0101454927157));
#169191=CARTESIAN_POINT('Ctrl Pts',(-19.9362268569848,-17.2094904340712,
19.0101487651583));
#169192=CARTESIAN_POINT('Ctrl Pts',(-19.936134573514,-17.2094267675529,
19.0101554538906));
#169193=CARTESIAN_POINT('Ctrl Pts',(-19.9360874389634,-17.2093942521714,
19.0101588701935));
#169194=CARTESIAN_POINT('Ctrl Pts',(-19.9359910413571,-17.2093277588489,
19.0101658570264));
#169195=CARTESIAN_POINT('Ctrl Pts',(-19.9359417782042,-17.2092937811012,
19.0101694275615));
#169196=CARTESIAN_POINT('Ctrl Pts',(-19.9358409654384,-17.2092242548982,
19.0101767343007));
#169197=CARTESIAN_POINT('Ctrl Pts',(-19.9357894157444,-17.2091887066794,
19.0101804705084));
#169198=CARTESIAN_POINT('Ctrl Pts',(-19.9356838552768,-17.2091159200133,
19.0101881212419));
#169199=CARTESIAN_POINT('Ctrl Pts',(-19.9356298443481,-17.2090786817886,
19.0101920357762));
#169200=CARTESIAN_POINT('Ctrl Pts',(-19.9355191677221,-17.2090023825796,
19.0102000571928));
#169201=CARTESIAN_POINT('Ctrl Pts',(-19.9354625017867,-17.2089633218038,
19.0102041640894));
#169202=CARTESIAN_POINT('Ctrl Pts',(-19.9353462991118,-17.208883229718,
19.0102125858786));
#169203=CARTESIAN_POINT('Ctrl Pts',(-19.9352867622703,-17.2088421987604,
19.0102169007752));
#169204=CARTESIAN_POINT('Ctrl Pts',(-19.935164576904,-17.2087580016018,
19.0102257560118));
#169205=CARTESIAN_POINT('Ctrl Pts',(-19.9351019281163,-17.2087148357014,
19.0102302963669));
#169206=CARTESIAN_POINT('Ctrl Pts',(-19.9349732486296,-17.2086261839453,
19.010239622093));
#169207=CARTESIAN_POINT('Ctrl Pts',(-19.934907217613,-17.2085806984222,
19.0102444074825));
#169208=CARTESIAN_POINT('Ctrl Pts',(-19.9347714693171,-17.208487199462,
19.0102542453208));
#169209=CARTESIAN_POINT('Ctrl Pts',(-19.9347017517542,-17.2084391864635,
19.010259297785));
#169210=CARTESIAN_POINT('Ctrl Pts',(-19.9345582862882,-17.2083403975427,
19.0102696946925));
#169211=CARTESIAN_POINT('Ctrl Pts',(-19.9344845380962,-17.2082896221537,
19.010275039151));
#169212=CARTESIAN_POINT('Ctrl Pts',(-19.9343326207668,-17.2081850417752,
19.0102860483358));
#169213=CARTESIAN_POINT('Ctrl Pts',(-19.9342544512108,-17.2081312373478,
19.0102917130858));
#169214=CARTESIAN_POINT('Ctrl Pts',(-19.9340932450911,-17.2080202944855,
19.0103033951579));
#169215=CARTESIAN_POINT('Ctrl Pts',(-19.9340102080862,-17.2079631567398,
19.0103094125041));
#169216=CARTESIAN_POINT('Ctrl Pts',(-19.9338387550747,-17.2078451980006,
19.0103218368465));
#169217=CARTESIAN_POINT('Ctrl Pts',(-19.9337503385751,-17.2077843778347,
19.0103282438691));
#169218=CARTESIAN_POINT('Ctrl Pts',(-19.933567535728,-17.2076586514248,
19.0103414903509));
#169219=CARTESIAN_POINT('Ctrl Pts',(-19.9334731486601,-17.2075937460657,
19.0103483298514));
#169220=CARTESIAN_POINT('Ctrl Pts',(-19.933277716491,-17.2074593803058,
19.0103624911224));
#169221=CARTESIAN_POINT('Ctrl Pts',(-19.9331766706376,-17.2073899210335,
19.0103698129347));
#169222=CARTESIAN_POINT('Ctrl Pts',(-19.9329671231812,-17.2072459041853,
19.0103849965917));
#169223=CARTESIAN_POINT('Ctrl Pts',(-19.9328586171266,-17.207171345526,
19.0103928587434));
#169224=CARTESIAN_POINT('Ctrl Pts',(-19.9326331949499,-17.2070164802836,
19.0104091921796));
#169225=CARTESIAN_POINT('Ctrl Pts',(-19.9325162787512,-17.2069361760419,
19.0104176634505));
#169226=CARTESIAN_POINT('Ctrl Pts',(-19.9272497993052,-17.2033196577882,
19.0107992449026));
#169227=CARTESIAN_POINT('Ctrl Pts',(-19.9220846628211,-17.1998062734238,
19.0111732180024));
#169228=CARTESIAN_POINT('Ctrl Pts',(-19.9101877741213,-17.1917906641275,
19.0120340236554));
#169229=CARTESIAN_POINT('Ctrl Pts',(-19.9034456171162,-17.1873041248282,
19.0125214411161));
#169230=CARTESIAN_POINT('Ctrl Pts',(-19.8836696498884,-17.1743073949284,
19.0139500135982));
#169231=CARTESIAN_POINT('Ctrl Pts',(-19.8705677326564,-17.1659022784926,
19.0148950717558));
#169232=CARTESIAN_POINT('Ctrl Pts',(-19.7583330406485,-17.0956366784126,
19.0229804842031));
#169233=CARTESIAN_POINT('Ctrl Pts',(-19.6543443052849,-17.0419472486438,
19.0304217705248));
#169234=CARTESIAN_POINT('Ctrl Pts',(-19.3961508642354,-16.9346390465809,
19.0486855589556));
#169235=CARTESIAN_POINT('Ctrl Pts',(-19.2391284953313,-16.8897113999657,
19.0596483580096));
#169236=CARTESIAN_POINT('Ctrl Pts',(-19.0465105225225,-16.8579422165123,
19.0720522004168));
#169237=CARTESIAN_POINT('Ctrl Pts',(-19.0143918159746,-16.8534001039692,
19.0740847793175));
#169238=CARTESIAN_POINT('Ctrl Pts',(-18.9749949391518,-16.848749473756,
19.0765241962998));
#169239=CARTESIAN_POINT('Ctrl Pts',(-18.9678059825353,-16.8479381893932,
19.076967147741));
#169240=CARTESIAN_POINT('Ctrl Pts',(-18.9565279679913,-16.8467239650184,
19.077658479534));
#169241=CARTESIAN_POINT('Ctrl Pts',(-18.9524417342475,-16.8462960584621,
19.0779082281117));
#169242=CARTESIAN_POINT('Ctrl Pts',(-18.9448005496863,-16.8455183628175,
19.0783738492124));
#169243=CARTESIAN_POINT('Ctrl Pts',(-18.9412459985656,-16.8451656790714,
19.078589876769));
#169244=CARTESIAN_POINT('Ctrl Pts',(-18.9331286933074,-16.8443810192673,
19.0790819176182));
#169245=CARTESIAN_POINT('Ctrl Pts',(-18.928565427183,-16.8439548629371,
19.0793576011537));
#169246=CARTESIAN_POINT('Ctrl Pts',(-18.914530882507,-16.8426901585234,
19.0802027353073));
#169247=CARTESIAN_POINT('Ctrl Pts',(-18.9050551594078,-16.8419005836319,
19.0807695059423));
#169248=CARTESIAN_POINT('Ctrl Pts',(-18.7758513589094,-16.8320106096061,
19.088449157343));
#169249=CARTESIAN_POINT('Ctrl Pts',(-18.6555472623204,-16.8330473991746,
19.0950401932027));
#169250=CARTESIAN_POINT('Ctrl Pts',(-18.4276535225468,-16.8544595463309,
19.1074983522716));
#169251=CARTESIAN_POINT('Ctrl Pts',(-18.3202880838129,-16.8729700285359,
19.1133590281367));
#169252=CARTESIAN_POINT('Ctrl Pts',(-18.1422882174557,-16.9179979169929,
19.1235738221552));
#169253=CARTESIAN_POINT('Ctrl Pts',(-18.0707816757159,-16.9401781713834,
19.1278173256892));
#169254=CARTESIAN_POINT('Ctrl Pts',(-17.9829885357855,-16.9726002433909,
19.1332820626392));
#169255=CARTESIAN_POINT('Ctrl Pts',(-17.9654610696231,-16.9793394882244,
19.1343859786424));
#169256=CARTESIAN_POINT('Ctrl Pts',(-17.9400880896355,-16.9894847866668,
19.1360038334498));
#169257=CARTESIAN_POINT('Ctrl Pts',(-17.9321695884559,-16.9927067417471,
19.1365115750622));
#169258=CARTESIAN_POINT('Ctrl Pts',(-17.9183127948655,-16.9984429965021,
19.1374051606786));
#169259=CARTESIAN_POINT('Ctrl Pts',(-17.9123660346458,-17.0009366468277,
19.1377903006078));
#169260=CARTESIAN_POINT('Ctrl Pts',(-17.900835242363,-17.0058339113044,
19.1385403385857));
#169261=CARTESIAN_POINT('Ctrl Pts',(-17.8952499828551,-17.0082344879853,
19.1389051301054));
#169262=CARTESIAN_POINT('Ctrl Pts',(-17.8819136279847,-17.0140347135778,
19.1397797771414));
#169263=CARTESIAN_POINT('Ctrl Pts',(-17.8741724737975,-17.0174568346295,
19.1402903981253));
#169264=CARTESIAN_POINT('Ctrl Pts',(-17.8462580594494,-17.029997566416,
19.1421424261568));
#169265=CARTESIAN_POINT('Ctrl Pts',(-17.8262081668378,-17.0393858107417,
19.143493068673));
#169266=CARTESIAN_POINT('Ctrl Pts',(-17.6397246871797,-17.1302984564891,
19.1562520690146));
#169267=CARTESIAN_POINT('Ctrl Pts',(-17.4845546907044,-17.2330195161703,
19.1684571195222));
#169268=CARTESIAN_POINT('Ctrl Pts',(-17.284157874126,-17.4072996309446,
19.1859916809906));
#169269=CARTESIAN_POINT('Ctrl Pts',(-17.2265910897872,-17.4634229881563,
19.1912698442899));
#169270=CARTESIAN_POINT('Ctrl Pts',(-17.1479917538631,-17.549299577346,
19.1986912316919));
#169271=CARTESIAN_POINT('Ctrl Pts',(-17.1243158052112,-17.5765336117748,
19.2009579947399));
#169272=CARTESIAN_POINT('Ctrl Pts',(-17.0965912909633,-17.6101216491536,
19.203637447941));
#169273=CARTESIAN_POINT('Ctrl Pts',(-17.0918669906679,-17.6159071991872,
19.2040949456575));
#169274=CARTESIAN_POINT('Ctrl Pts',(-17.0845593030779,-17.6249537715524,
19.2048038863541));
#169275=CARTESIAN_POINT('Ctrl Pts',(-17.0819547944477,-17.6281975432115,
19.2050568121235));
#169276=CARTESIAN_POINT('Ctrl Pts',(-17.0771355599793,-17.634236006639,
19.2055252520864));
#169277=CARTESIAN_POINT('Ctrl Pts',(-17.0749183543924,-17.6370285903149,
19.2057409402898));
#169278=CARTESIAN_POINT('Ctrl Pts',(-17.0699130514561,-17.6433656112877,
19.206228254774));
#169279=CARTESIAN_POINT('Ctrl Pts',(-17.0671292243886,-17.6469133538681,
19.206499576062));
#169280=CARTESIAN_POINT('Ctrl Pts',(-17.0599715841504,-17.6560953980065,
19.2071980117624));
#169281=CARTESIAN_POINT('Ctrl Pts',(-17.0556148306113,-17.6617430097167,
19.2076239448919));
#169282=CARTESIAN_POINT('Ctrl Pts',(-17.0290541481358,-17.696535516794,
19.2102263355417));
#169283=CARTESIAN_POINT('Ctrl Pts',(-17.0075799347702,-17.7262326698287,
19.2123551159605));
#169284=CARTESIAN_POINT('Ctrl Pts',(-16.890539391678,-17.8972730372875,
19.2241944910592));
#169285=CARTESIAN_POINT('Ctrl Pts',(-16.8115572535784,-18.0492143334176,
19.2331708284439));
#169286=CARTESIAN_POINT('Ctrl Pts',(-16.7182073512736,-18.2982738125913,
19.2478021752191));
#169287=CARTESIAN_POINT('Ctrl Pts',(-16.6908195419361,-18.3896936088725,
19.2531477559489));
#169288=CARTESIAN_POINT('Ctrl Pts',(-16.6649450735421,-18.5034935746245,
19.2599434909318));
#169289=CARTESIAN_POINT('Ctrl Pts',(-16.6605202634838,-18.5244160488914,
19.2611982872611));
#169290=CARTESIAN_POINT('Ctrl Pts',(-16.6546830461206,-18.5542423340368,
19.2629960837188));
#169291=CARTESIAN_POINT('Ctrl Pts',(-16.653009285874,-18.5630940995251,
19.2635307474836));
#169292=CARTESIAN_POINT('Ctrl Pts',(-16.6502205088103,-18.578376361172,
19.2644558566976));
#169293=CARTESIAN_POINT('Ctrl Pts',(-16.6490786283418,-18.5848018737439,
19.2648454413258));
#169294=CARTESIAN_POINT('Ctrl Pts',(-16.646949950947,-18.5971103341509,
19.2655929344194));
#169295=CARTESIAN_POINT('Ctrl Pts',(-16.6459582705416,-18.60299238248,19.2659506834388));
#169296=CARTESIAN_POINT('Ctrl Pts',(-16.643445826809,-18.6182887609983,
19.2668824354375));
#169297=CARTESIAN_POINT('Ctrl Pts',(-16.6419638054525,-18.6277092382887,
19.267457662252));
#169298=CARTESIAN_POINT('Ctrl Pts',(-16.6371349041361,-18.6598157692268,
19.2694230470449));
#169299=CARTESIAN_POINT('Ctrl Pts',(-16.6340930910722,-18.6825454325821,
19.2708227967042));
#169300=CARTESIAN_POINT('Ctrl Pts',(-16.6108742340152,-18.8804510061067,
19.2830870664644));
#169301=CARTESIAN_POINT('Ctrl Pts',(-16.6122925456928,-19.0574323901985,
19.2946629473972));
#169302=CARTESIAN_POINT('Ctrl Pts',(-16.6470546155064,-19.3178097049176,
19.3120182724925));
#169303=CARTESIAN_POINT('Ctrl Pts',(-16.663726550155,-19.4026967079917,
19.3177125441004));
#169304=CARTESIAN_POINT('Ctrl Pts',(-16.6950510195942,-19.5227848349962,
19.3256351705694));
#169305=CARTESIAN_POINT('Ctrl Pts',(-16.7055318301905,-19.5589806934331,
19.3280046819857));
#169306=CARTESIAN_POINT('Ctrl Pts',(-16.7192706293368,-19.602085967026,
19.330788619515));
#169307=CARTESIAN_POINT('Ctrl Pts',(-16.7216060145436,-19.609279737099,
19.331251941267));
#169308=CARTESIAN_POINT('Ctrl Pts',(-16.7252920372529,-19.6204300980979,
19.3319679224975));
#169309=CARTESIAN_POINT('Ctrl Pts',(-16.7266158990158,-19.6243953803083,
19.3322221117235));
#169310=CARTESIAN_POINT('Ctrl Pts',(-16.729090130019,-19.6317338556515,
19.3326917080113));
#169311=CARTESIAN_POINT('Ctrl Pts',(-16.7302372613418,-19.6351080359124,
19.3329072965428));
#169312=CARTESIAN_POINT('Ctrl Pts',(-16.7328464284257,-19.6427195338902,
19.3333928922242));
#169313=CARTESIAN_POINT('Ctrl Pts',(-16.7343134001171,-19.6469551025934,
19.3336626035485));
#169314=CARTESIAN_POINT('Ctrl Pts',(-16.7386725704694,-19.6594131906992,
19.3344544967689));
#169315=CARTESIAN_POINT('Ctrl Pts',(-16.7416021509993,-19.6676226593819,
19.3349745164931));
#169316=CARTESIAN_POINT('Ctrl Pts',(-16.7628005644233,-19.7258869357973,
19.338653853538));
#169317=CARTESIAN_POINT('Ctrl Pts',(-16.78290438591,-19.7752588447044,19.3417120238881));
#169318=CARTESIAN_POINT('Ctrl Pts',(-16.8121247842516,-19.8399169720583,
19.3457025569934));
#169319=CARTESIAN_POINT('Ctrl Pts',(-16.8195989883718,-19.8559190699414,
19.346688934853));
#169320=CARTESIAN_POINT('Ctrl Pts',(-16.8444620114034,-19.9074581669546,
19.3498674665437));
#169321=CARTESIAN_POINT('Ctrl Pts',(-16.8626472551777,-19.942602440803,
19.3520375368829));
#169322=CARTESIAN_POINT('Ctrl Pts',(-16.8864672287967,-19.9856364239982,
19.3547212921827));
#169323=CARTESIAN_POINT('Ctrl Pts',(-16.8911846929554,-19.9940236768286,
19.355245625933));
#169324=CARTESIAN_POINT('Ctrl Pts',(-16.9501050331804,-20.0971274527719,
19.3617101411828));
#169325=CARTESIAN_POINT('Ctrl Pts',(-17.0114956169318,-20.1875467927259,
19.367587427947));
#169326=CARTESIAN_POINT('Ctrl Pts',(-17.1265936104555,-20.3317143463212,
19.3778472346854));
#169327=CARTESIAN_POINT('Ctrl Pts',(-17.1767131752537,-20.3880442198723,
19.3821195574633));
#169328=CARTESIAN_POINT('Ctrl Pts',(-17.2429883901071,-20.4549732852334,
19.3876190271278));
#169329=CARTESIAN_POINT('Ctrl Pts',(-17.2564296321415,-20.4681893321695,
19.3887271038609));
#169330=CARTESIAN_POINT('Ctrl Pts',(-17.2762301306267,-20.4871447220901,
19.3903499471542));
#169331=CARTESIAN_POINT('Ctrl Pts',(-17.2824508029408,-20.4930279799684,
19.3908584617271));
#169332=CARTESIAN_POINT('Ctrl Pts',(-17.293420241668,-20.5032770767062,
19.3917529404323));
#169333=CARTESIAN_POINT('Ctrl Pts',(-17.2981536205257,-20.5076592756639,
19.3921381960605));
#169334=CARTESIAN_POINT('Ctrl Pts',(-17.3073839052033,-20.5161267304554,
19.392888111906));
#169335=CARTESIAN_POINT('Ctrl Pts',(-17.3118785190972,-20.520214399633,
19.3932526639616));
#169336=CARTESIAN_POINT('Ctrl Pts',(-17.3226657296067,-20.5299404185947,
19.3941261748342));
#169337=CARTESIAN_POINT('Ctrl Pts',(-17.3289745711554,-20.5355605225199,
19.3946358946464));
#169338=CARTESIAN_POINT('Ctrl Pts',(-17.3518645674362,-20.5557071424222,
19.3964812864004));
#169339=CARTESIAN_POINT('Ctrl Pts',(-17.3686382833067,-20.5700118286111,
19.3978261078191));
#169340=CARTESIAN_POINT('Ctrl Pts',(-17.5292301135471,-20.7026895677109,
19.4106359539574));
#169341=CARTESIAN_POINT('Ctrl Pts',(-17.6878329156799,-20.8018353899521,
19.4229069649804));
#169342=CARTESIAN_POINT('Ctrl Pts',(-17.9298612685993,-20.9119498112448,
19.440461057947));
#169343=CARTESIAN_POINT('Ctrl Pts',(-18.0042246878999,-20.9408368607195,
19.4456970283631));
#169344=CARTESIAN_POINT('Ctrl Pts',(-18.1141992882798,-20.9765556763063,
19.4530672197101));
#169345=CARTESIAN_POINT('Ctrl Pts',(-18.1486332409006,-20.9867787892037,
19.4553232345235));
#169346=CARTESIAN_POINT('Ctrl Pts',(-18.190515166339,-20.9980617960486,
19.4579917297661));
#169347=CARTESIAN_POINT('Ctrl Pts',(-18.1977277797753,-20.9999640493162,
19.4584485996968));
#169348=CARTESIAN_POINT('Ctrl Pts',(-18.2089762261266,-21.0028672125696,
19.4591567811294));
#169349=CARTESIAN_POINT('Ctrl Pts',(-18.2130051255652,-21.0038943998716,
19.4594095703964));
#169350=CARTESIAN_POINT('Ctrl Pts',(-18.2204951135059,-21.0057805257495,
19.459877886552));
#169351=CARTESIAN_POINT('Ctrl Pts',(-18.2239553130831,-21.0066425806023,
19.4600935866421));
#169352=CARTESIAN_POINT('Ctrl Pts',(-18.2317991610488,-21.0085757170738,
19.4605810919392));
#169353=CARTESIAN_POINT('Ctrl Pts',(-18.2361840544666,-21.0096415256161,
19.4608525911412));
#169354=CARTESIAN_POINT('Ctrl Pts',(-18.2475181281418,-21.0123580764884,
19.4615517891884));
#169355=CARTESIAN_POINT('Ctrl Pts',(-18.2544723794457,-21.0139877010777,
19.4619783024377));
#169356=CARTESIAN_POINT('Ctrl Pts',(-18.2973043473353,-21.0237963221259,
19.4645906634016));
#169357=CARTESIAN_POINT('Ctrl Pts',(-18.3333843796563,-21.0310744540621,
19.4667284137824));
#169358=CARTESIAN_POINT('Ctrl Pts',(-18.5372432908988,-21.0666926058822,
19.4785484183481));
#169359=CARTESIAN_POINT('Ctrl Pts',(-18.7077821135932,-21.0756672566111,
19.4875020754519));
#169360=CARTESIAN_POINT('Ctrl Pts',(-18.97292910807,-21.0576441602349,19.5021196386494));
#169361=CARTESIAN_POINT('Ctrl Pts',(-19.0677297480415,-21.0447125498654,
19.5074781566405));
#169362=CARTESIAN_POINT('Ctrl Pts',(-19.1822988813553,-21.0211002048489,
19.5142895635556));
#169363=CARTESIAN_POINT('Ctrl Pts',(-19.203204364688,-21.0164599195375,
19.5155460379922));
#169364=CARTESIAN_POINT('Ctrl Pts',(-19.2328040485607,-21.0094170129046,
19.5173458251005));
#169365=CARTESIAN_POINT('Ctrl Pts',(-19.241559262988,-21.0072746372635,
19.5178807758486));
#169366=CARTESIAN_POINT('Ctrl Pts',(-19.2566304395562,-21.0034845908973,
19.5188062250182));
#169367=CARTESIAN_POINT('Ctrl Pts',(-19.2629530005789,-21.0018634892955,
19.519195860917));
#169368=CARTESIAN_POINT('Ctrl Pts',(-19.2750381887715,-20.9987052177558,
19.519943343238));
#169369=CARTESIAN_POINT('Ctrl Pts',(-19.2808020232943,-20.9971728817603,
19.5203010296874));
#169370=CARTESIAN_POINT('Ctrl Pts',(-19.2957596466676,-20.993128593397,
19.5212323794074));
#169371=CARTESIAN_POINT('Ctrl Pts',(-19.3049430088916,-20.9905788950537,
19.5218072644184));
#169372=CARTESIAN_POINT('Ctrl Pts',(-19.3361297546822,-20.9816928469804,
19.5237702306762));
#169373=CARTESIAN_POINT('Ctrl Pts',(-19.3580468242027,-20.9750617368602,
19.5251678716111));
#169374=CARTESIAN_POINT('Ctrl Pts',(-19.548199806244,-20.9141461138245,
19.5374569004443));
#169375=CARTESIAN_POINT('Ctrl Pts',(-19.7091002162916,-20.8393511398131,
19.5490637032728));
#169376=CARTESIAN_POINT('Ctrl Pts',(-19.931755790896,-20.6997087010685,
19.5664275169328));
#169377=CARTESIAN_POINT('Ctrl Pts',(-20.0018543448731,-20.6495428984462,
19.5721007360978));
#169378=CARTESIAN_POINT('Ctrl Pts',(-20.0978873299732,-20.5715412053722,
19.5799981582999));
#169379=CARTESIAN_POINT('Ctrl Pts',(-20.1264344625499,-20.5470639596866,
19.5823626094695));
#169380=CARTESIAN_POINT('Ctrl Pts',(-20.1599214405646,-20.5167664933397,
19.5851414124359));
#169381=CARTESIAN_POINT('Ctrl Pts',(-20.1654993780857,-20.511665242236,
19.5856044546681));
#169382=CARTESIAN_POINT('Ctrl Pts',(-20.1741189508785,-20.5036970950474,
19.586320098126));
#169383=CARTESIAN_POINT('Ctrl Pts',(-20.1771795548684,-20.5008509420098,
19.5865742268315));
#169384=CARTESIAN_POINT('Ctrl Pts',(-20.1828344231619,-20.4955609855554,
19.5870437673393));
#169385=CARTESIAN_POINT('Ctrl Pts',(-20.1854309222924,-20.4931197163027,
19.5872593602544));
#169386=CARTESIAN_POINT('Ctrl Pts',(-20.1912800867429,-20.4875923455621,
19.587745036444));
#169387=CARTESIAN_POINT('Ctrl Pts',(-20.1945291111164,-20.4845024696222,
19.5880148234617));
#169388=CARTESIAN_POINT('Ctrl Pts',(-20.2040695793198,-20.4753714283376,
19.5888071448289));
#169389=CARTESIAN_POINT('Ctrl Pts',(-20.2103336212087,-20.4693015921458,
19.5893275135088));
#169390=CARTESIAN_POINT('Ctrl Pts',(-20.2546644095094,-20.4258107519157,
19.5930128190976));
#169391=CARTESIAN_POINT('Ctrl Pts',(-20.291344719402,-20.3869971516115,
19.5960762463696));
#169392=CARTESIAN_POINT('Ctrl Pts',(-20.3355344069428,-20.3365445712775,
19.5998479353816));
#169393=CARTESIAN_POINT('Ctrl Pts',(-20.3444475999265,-20.3261668988453,
19.6006131056275));
#169394=CARTESIAN_POINT('Ctrl Pts',(-20.3868892527341,-20.2757717336107,
19.6042819764768));
#169395=CARTESIAN_POINT('Ctrl Pts',(-20.4190314109285,-20.2346082846777,
19.6071384888453));
#169396=CARTESIAN_POINT('Ctrl Pts',(-20.5137302287811,-20.103617783417,
19.6159390577793));
#169397=CARTESIAN_POINT('Ctrl Pts',(-20.5708677304338,-20.0101017306773,
19.6218309140156));
#169398=CARTESIAN_POINT('Ctrl Pts',(-20.6549212413534,-19.8450280149816,
19.6321302259222));
#169399=CARTESIAN_POINT('Ctrl Pts',(-20.6856664651168,-19.7756708746541,
19.6364278586011));
#169400=CARTESIAN_POINT('Ctrl Pts',(-20.71934941304,-19.6871424346948,19.6419578335176));
#169401=CARTESIAN_POINT('Ctrl Pts',(-20.7258375543615,-19.6693770374386,
19.6430695541002));
#169402=CARTESIAN_POINT('Ctrl Pts',(-20.7349196704995,-19.6434354486702,
19.6446967649728));
#169403=CARTESIAN_POINT('Ctrl Pts',(-20.7377034740661,-19.6353263438405,
19.6452059550948));
#169404=CARTESIAN_POINT('Ctrl Pts',(-20.7424958172422,-19.6210853339409,
19.6461012150884));
#169405=CARTESIAN_POINT('Ctrl Pts',(-20.7445257366996,-19.6149607021688,
19.6464865725825));
#169406=CARTESIAN_POINT('Ctrl Pts',(-20.7484115458999,-19.603054524388,
19.6472363846186));
#169407=CARTESIAN_POINT('Ctrl Pts',(-20.7502706244743,-19.597274079495,
19.6476007295784));
#169408=CARTESIAN_POINT('Ctrl Pts',(-20.7546531721575,-19.5834435284464,
19.6484732565121));
#169409=CARTESIAN_POINT('Ctrl Pts',(-20.757153425305,-19.5753862255621,
19.6489821956122));
#169410=CARTESIAN_POINT('Ctrl Pts',(-20.7659891983743,-19.5462989926952,
19.6508218766976));
#169411=CARTESIAN_POINT('Ctrl Pts',(-20.7720453441935,-19.5251862812417,
19.6521616945787));
#169412=CARTESIAN_POINT('Ctrl Pts',(-20.8265422864656,-19.3234062360452,
19.665013519989));
#169413=CARTESIAN_POINT('Ctrl Pts',(-20.8511563473453,-19.1371933086967,
19.677339284135));
#169414=CARTESIAN_POINT('Ctrl Pts',(-20.8509463099948,-18.887209432531,
19.6938412930769));
#169415=CARTESIAN_POINT('Ctrl Pts',(-20.8480800908105,-18.8242283125836,
19.6979837889211));
#169416=CARTESIAN_POINT('Ctrl Pts',(-20.8379188596087,-18.7117861112607,
19.7052635376531));
#169417=CARTESIAN_POINT('Ctrl Pts',(-20.8316744040226,-18.6622755763367,
19.7084278926623));
#169418=CARTESIAN_POINT('Ctrl Pts',(-20.8224344764443,-18.6053135194725,
19.711986642042));
#169419=CARTESIAN_POINT('Ctrl Pts',(-20.8211403742769,-18.5976059529908,
19.7124664260019));
#169420=CARTESIAN_POINT('Ctrl Pts',(-20.8190058158766,-18.5853100723495,
19.7132288325168));
#169421=CARTESIAN_POINT('Ctrl Pts',(-20.8181928414099,-18.5807171481805,
19.7135129487449));
#169422=CARTESIAN_POINT('Ctrl Pts',(-20.8167271896856,-18.57259343029,19.7140142493685));
#169423=CARTESIAN_POINT('Ctrl Pts',(-20.8160807013085,-18.5690615639899,
19.7142317815118));
#169424=CARTESIAN_POINT('Ctrl Pts',(-20.8146926433247,-18.5615858259236,
19.7146913321523));
#169425=CARTESIAN_POINT('Ctrl Pts',(-20.8139488463912,-18.5576424207429,
19.7149332222231));
#169426=CARTESIAN_POINT('Ctrl Pts',(-20.8119140369176,-18.5470203389648,
19.7155834406428));
#169427=CARTESIAN_POINT('Ctrl Pts',(-20.8106020277839,-18.5403456647312,
19.7159905890604));
#169428=CARTESIAN_POINT('Ctrl Pts',(-20.803970731503,-18.5074484527189,
19.7179907208875));
#169429=CARTESIAN_POINT('Ctrl Pts',(-20.7981865537565,-18.4813207785408,
19.7195586651717));
#169430=CARTESIAN_POINT('Ctrl Pts',(-20.7800922390971,-18.4063518374011,
19.7240162882166));
#169431=CARTESIAN_POINT('Ctrl Pts',(-20.7665321585851,-18.357829091126,
19.7268505746596));
#169432=CARTESIAN_POINT('Ctrl Pts',(-20.7422796918877,-18.2816442556438,
19.7312843315893));
#169433=CARTESIAN_POINT('Ctrl Pts',(-20.7327195762116,-18.2536570392336,
19.7329094971324));
#169434=CARTESIAN_POINT('Ctrl Pts',(-20.7225805414791,-18.2258895193907,
19.7345260867578));
#169435=CARTESIAN_POINT('Origin',(-18.734,-18.952,0.));
#169436=CARTESIAN_POINT('',(-20.7225805788317,-18.2258896216872,20.755413772291));
#169437=CARTESIAN_POINT('',(-20.7225805737622,-18.2258896078036,20.5336910569984));
#169438=CARTESIAN_POINT('',(-20.7225805737622,-18.2258896078036,0.));
#169439=CARTESIAN_POINT('Ctrl Pts',(-20.7225805788317,-18.2258896216873,
20.755413772291));
#169440=CARTESIAN_POINT('Ctrl Pts',(-20.7319594498863,-18.2515753044535,
20.7536068528629));
#169441=CARTESIAN_POINT('Ctrl Pts',(-20.7408447755382,-18.277453954992,
20.7517982257749));
#169442=CARTESIAN_POINT('Ctrl Pts',(-20.7725200329136,-18.375887392365,
20.7449760667245));
#169443=CARTESIAN_POINT('Ctrl Pts',(-20.7918958199826,-18.4494703633789,
20.7399904291453));
#169444=CARTESIAN_POINT('Ctrl Pts',(-20.8143280497788,-18.5581190996573,
20.732925459953));
#169445=CARTESIAN_POINT('Ctrl Pts',(-20.8205389606962,-18.5924691228743,
20.7307345037727));
#169446=CARTESIAN_POINT('Ctrl Pts',(-20.8270336495132,-18.6342676521286,
20.7281324773479));
#169447=CARTESIAN_POINT('Ctrl Pts',(-20.8281309523597,-18.6415821188121,
20.7276795047987));
#169448=CARTESIAN_POINT('Ctrl Pts',(-20.8297832008251,-18.6530034342135,
20.7269760486136));
#169449=CARTESIAN_POINT('Ctrl Pts',(-20.8303644475973,-18.6571063331596,
20.7267241180626));
#169450=CARTESIAN_POINT('Ctrl Pts',(-20.8314236225145,-18.6647442395575,
20.7262565992299));
#169451=CARTESIAN_POINT('Ctrl Pts',(-20.8319046584193,-18.6682787131087,
20.726040842706));
#169452=CARTESIAN_POINT('Ctrl Pts',(-20.8329764089929,-18.6763053106689,
20.7255521954007));
#169453=CARTESIAN_POINT('Ctrl Pts',(-20.8335616364932,-18.680798114541,
20.7252796168897));
#169454=CARTESIAN_POINT('Ctrl Pts',(-20.835259186705,-18.6941651342987,
20.7244713321322));
#169455=CARTESIAN_POINT('Ctrl Pts',(-20.8363297185985,-18.7030446860307,
20.7239379246181));
#169456=CARTESIAN_POINT('Ctrl Pts',(-20.8440773295531,-18.7709246959512,
20.7198853747505));
#169457=CARTESIAN_POINT('Ctrl Pts',(-20.8483264214979,-18.8301815006446,
20.7164921316396));
#169458=CARTESIAN_POINT('Ctrl Pts',(-20.8506770340003,-18.9098227212251,
20.7120328634702));
#169459=CARTESIAN_POINT('Ctrl Pts',(-20.8509840406084,-18.9301095183887,
20.710905785112));
#169460=CARTESIAN_POINT('Ctrl Pts',(-20.8511051846752,-19.0901947745642,
20.7020608620862));
#169461=CARTESIAN_POINT('Ctrl Pts',(-20.8373639001827,-19.2296587432821,
20.6946257986704));
#169462=CARTESIAN_POINT('Ctrl Pts',(-20.7922497624043,-19.4554696483924,
20.6818795550826));
#169463=CARTESIAN_POINT('Ctrl Pts',(-20.7688587852084,-19.542948911302,
20.6767638662586));
#169464=CARTESIAN_POINT('Ctrl Pts',(-20.7355595809391,-19.6416641653536,
20.6706561060802));
#169465=CARTESIAN_POINT('Ctrl Pts',(-20.7310458544951,-19.6546273968654,
20.6698473346312));
#169466=CARTESIAN_POINT('Ctrl Pts',(-20.7236045398111,-19.6753474230732,
20.6685434430718));
#169467=CARTESIAN_POINT('Ctrl Pts',(-20.720756848974,-19.6831326414369,
20.6680509769946));
#169468=CARTESIAN_POINT('Ctrl Pts',(-20.7156191670394,-19.6969267247075,
20.6671737914043));
#169469=CARTESIAN_POINT('Ctrl Pts',(-20.7133473731812,-19.7029422902152,
20.6667896842574));
#169470=CARTESIAN_POINT('Ctrl Pts',(-20.7085566075865,-19.7154551479226,
20.6659873958386));
#169471=CARTESIAN_POINT('Ctrl Pts',(-20.7060328946614,-19.7219505308911,
20.6655690589631));
#169472=CARTESIAN_POINT('Ctrl Pts',(-20.6993949321713,-19.7387881859352,
20.6644796971704));
#169473=CARTESIAN_POINT('Ctrl Pts',(-20.6952311444706,-19.7491105817125,
20.663807008012));
#169474=CARTESIAN_POINT('Ctrl Pts',(-20.6767885703737,-19.7938119503979,
20.6608724366708));
#169475=CARTESIAN_POINT('Ctrl Pts',(-20.6616864867406,-19.8278420644715,
20.6585827761449));
#169476=CARTESIAN_POINT('Ctrl Pts',(-20.619174332485,-19.9172036395332,
20.6524167790992));
#169477=CARTESIAN_POINT('Ctrl Pts',(-20.5902290846934,-19.9717611426819,
20.6484906701569));
#169478=CARTESIAN_POINT('Ctrl Pts',(-20.4847189653704,-20.1512159401868,
20.6350415698986));
#169479=CARTESIAN_POINT('Ctrl Pts',(-20.3975957566837,-20.2694140260674,
20.6252362741343));
#169480=CARTESIAN_POINT('Ctrl Pts',(-20.2858382990858,-20.3920930540122,
20.614403749887));
#169481=CARTESIAN_POINT('Ctrl Pts',(-20.2724921822452,-20.4063424454815,
20.6131349579298));
#169482=CARTESIAN_POINT('Ctrl Pts',(-20.2223182615595,-20.4584484551818,
20.6084615483341));
#169483=CARTESIAN_POINT('Ctrl Pts',(-20.1842716892352,-20.4951108945269,
20.6051053299749));
#169484=CARTESIAN_POINT('Ctrl Pts',(-20.138409392091,-20.5361082115037,
20.6013107909744));
#169485=CARTESIAN_POINT('Ctrl Pts',(-20.1318927170487,-20.5418617939658,
20.6007772680363));
#169486=CARTESIAN_POINT('Ctrl Pts',(-20.1219663773764,-20.5505175565522,
20.5999733611395));
#169487=CARTESIAN_POINT('Ctrl Pts',(-20.118582734132,-20.5534492488146,
20.5997008556792));
#169488=CARTESIAN_POINT('Ctrl Pts',(-20.1124893257787,-20.558695016444,
20.5992128912468));
#169489=CARTESIAN_POINT('Ctrl Pts',(-20.1097830088015,-20.56101299262,20.5989971462405));
#169490=CARTESIAN_POINT('Ctrl Pts',(-20.1038860686669,-20.5660380002131,
20.5985291750485));
#169491=CARTESIAN_POINT('Ctrl Pts',(-20.1006932791657,-20.5687424002105,
20.5982771415332));
#169492=CARTESIAN_POINT('Ctrl Pts',(-20.0916937761393,-20.5763195717387,
20.5975704278406));
#169493=CARTESIAN_POINT('Ctrl Pts',(-20.0858688111858,-20.581170703819,
20.5971173035557));
#169494=CARTESIAN_POINT('Ctrl Pts',(-20.0507102080234,-20.6101329930512,
20.5944071623565));
#169495=CARTESIAN_POINT('Ctrl Pts',(-20.0207562855254,-20.6334843026105,
20.5922014799787));
#169496=CARTESIAN_POINT('Ctrl Pts',(-19.9196809192604,-20.7079962177203,
20.5850331461083));
#169497=CARTESIAN_POINT('Ctrl Pts',(-19.8460095528,-20.755551813513,20.5802387771415));
#169498=CARTESIAN_POINT('Ctrl Pts',(-19.6172811145266,-20.8838391130274,
20.5659714918296));
#169499=CARTESIAN_POINT('Ctrl Pts',(-19.4549978447177,-20.9500848969404,
20.5565785128704));
#169500=CARTESIAN_POINT('Ctrl Pts',(-19.264170593288,-21.0016681998836,
20.5450925586047));
#169501=CARTESIAN_POINT('Ctrl Pts',(-19.241817119652,-21.0073204857568,
20.5437418553941));
#169502=CARTESIAN_POINT('Ctrl Pts',(-19.2100738002255,-21.0147976335202,
20.5418146221661));
#169503=CARTESIAN_POINT('Ctrl Pts',(-19.2007565735709,-21.016925818666,
20.5412478413817));
#169504=CARTESIAN_POINT('Ctrl Pts',(-19.1855972553012,-21.0202805780205,
20.5403237679748));
#169505=CARTESIAN_POINT('Ctrl Pts',(-19.1797637579931,-21.0215456751057,
20.5399677152002));
#169506=CARTESIAN_POINT('Ctrl Pts',(-19.1675440245699,-21.0241416779993,
20.5392208822395));
#169507=CARTESIAN_POINT('Ctrl Pts',(-19.1611568397807,-21.0254677686649,
20.5388299521328));
#169508=CARTESIAN_POINT('Ctrl Pts',(-19.1459514913743,-21.0285514241805,
20.5378979157298));
#169509=CARTESIAN_POINT('Ctrl Pts',(-19.1371281120967,-21.0302823604723,
20.5373559650466));
#169510=CARTESIAN_POINT('Ctrl Pts',(-19.1073845519166,-21.0359207989474,
20.5355251823452));
#169511=CARTESIAN_POINT('Ctrl Pts',(-19.0864170712646,-21.0395689391925,
20.5342281393105));
#169512=CARTESIAN_POINT('Ctrl Pts',(-18.9079848837578,-21.0678496769323,
20.523132286479));
#169513=CARTESIAN_POINT('Ctrl Pts',(-18.7482861853164,-21.074938602777,
20.5127600434867));
#169514=CARTESIAN_POINT('Ctrl Pts',(-18.4580291623978,-21.0550577038001,
20.4935418429057));
#169515=CARTESIAN_POINT('Ctrl Pts',(-18.327834767814,-21.0338375356172,
20.4848031189808));
#169516=CARTESIAN_POINT('Ctrl Pts',(-18.1852107812422,-20.9966924555746,
20.4756084986054));
#169517=CARTESIAN_POINT('Ctrl Pts',(-18.1700201228866,-20.9925547226939,
20.4746343977949));
#169518=CARTESIAN_POINT('Ctrl Pts',(-18.1492990980026,-20.9866615146536,
20.4733141354613));
#169519=CARTESIAN_POINT('Ctrl Pts',(-18.143728128247,-20.9850523218168,
20.4729600180005));
#169520=CARTESIAN_POINT('Ctrl Pts',(-18.1348888083314,-20.9824596593075,
20.4723995676275));
#169521=CARTESIAN_POINT('Ctrl Pts',(-18.1316161515394,-20.9814911548351,
20.4721923771189));
#169522=CARTESIAN_POINT('Ctrl Pts',(-18.124864557165,-20.9794753295323,
20.4717655975538));
#169523=CARTESIAN_POINT('Ctrl Pts',(-18.1213859719914,-20.9784269669583,
20.4715460767376));
#169524=CARTESIAN_POINT('Ctrl Pts',(-18.1131075513809,-20.9759087839327,
20.4710244962207));
#169525=CARTESIAN_POINT('Ctrl Pts',(-18.108310175003,-20.974430825148,20.470722911176));
#169526=CARTESIAN_POINT('Ctrl Pts',(-18.0921660941982,-20.9693942714715,
20.4697101479295));
#169527=CARTESIAN_POINT('Ctrl Pts',(-18.0808438912191,-20.9657570661299,
20.4690034223074));
#169528=CARTESIAN_POINT('Ctrl Pts',(-17.9458112460332,-20.9211197588971,
20.460610617561));
#169529=CARTESIAN_POINT('Ctrl Pts',(-17.8260924564993,-20.8688692962793,
20.4535207494897));
#169530=CARTESIAN_POINT('Ctrl Pts',(-17.5698440899828,-20.7275994400364,
20.4376243946124));
#169531=CARTESIAN_POINT('Ctrl Pts',(-17.4372537334809,-20.6332062600607,
20.4288424937918));
#169532=CARTESIAN_POINT('Ctrl Pts',(-17.2991230565875,-20.5087209211266,
20.4180452046454));
#169533=CARTESIAN_POINT('Ctrl Pts',(-17.2817679447368,-20.4925433651398,
20.416655948622));
#169534=CARTESIAN_POINT('Ctrl Pts',(-17.2577286955992,-20.4693679530358,
20.4146830356628));
#169535=CARTESIAN_POINT('Ctrl Pts',(-17.2508146540427,-20.4626103713148,
20.4141097737895));
#169536=CARTESIAN_POINT('Ctrl Pts',(-17.2396928871838,-20.4515903180152,
20.4131780217954));
#169537=CARTESIAN_POINT('Ctrl Pts',(-17.2354564877059,-20.4473568837989,
20.4128208134773));
#169538=CARTESIAN_POINT('Ctrl Pts',(-17.2266554700819,-20.4384870667187,
20.412073881593));
#169539=CARTESIAN_POINT('Ctrl Pts',(-17.2220941534652,-20.4338475094095,
20.4116840183707));
#169540=CARTESIAN_POINT('Ctrl Pts',(-17.2113459825874,-20.4228136885758,
20.4107587695479));
#169541=CARTESIAN_POINT('Ctrl Pts',(-17.2051779456261,-20.4164013403187,
20.410222571876));
#169542=CARTESIAN_POINT('Ctrl Pts',(-17.1847720438394,-20.3949177373855,
20.4084309937269));
#169543=CARTESIAN_POINT('Ctrl Pts',(-17.1707155232986,-20.3796765929037,
20.4071678726075));
#169544=CARTESIAN_POINT('Ctrl Pts',(-17.0968741218778,-20.2972139694611,
20.4003731490595));
#169545=CARTESIAN_POINT('Ctrl Pts',(-17.0412031231709,-20.2264476832418,
20.3946735584241));
#169546=CARTESIAN_POINT('Ctrl Pts',(-16.9134063284424,-20.0407945271189,
20.3800670199015));
#169547=CARTESIAN_POINT('Ctrl Pts',(-16.8474928229997,-19.9221143400743,
20.371014339092));
#169548=CARTESIAN_POINT('Ctrl Pts',(-16.7632115370659,-19.7287745988722,
20.3572224489953));
#169549=CARTESIAN_POINT('Ctrl Pts',(-16.7367684475921,-19.6580131598617,
20.3523635289208));
#169550=CARTESIAN_POINT('Ctrl Pts',(-16.7113174135762,-19.5769273899586,
20.3471145792649));
#169551=CARTESIAN_POINT('Ctrl Pts',(-16.7085358505008,-19.5678523158582,
20.3465315437632));
#169552=CARTESIAN_POINT('Ctrl Pts',(-16.7045027522383,-19.5543710610501,
20.3456722940923));
#169553=CARTESIAN_POINT('Ctrl Pts',(-16.7032043731267,-19.549979177435,
20.3453934460292));
#169554=CARTESIAN_POINT('Ctrl Pts',(-16.7009187949656,-19.5421547003413,
20.3448986132645));
#169555=CARTESIAN_POINT('Ctrl Pts',(-16.6999260225646,-19.5387237949614,
20.3446823072442));
#169556=CARTESIAN_POINT('Ctrl Pts',(-16.6978093309882,-19.5313388098229,
20.3442181594933));
#169557=CARTESIAN_POINT('Ctrl Pts',(-16.6966882472189,-19.5273839759487,
20.3439704835246));
#169558=CARTESIAN_POINT('Ctrl Pts',(-16.6936233321182,-19.5164506446258,
20.3432881531373));
#169559=CARTESIAN_POINT('Ctrl Pts',(-16.6917037686742,-19.5094653209097,
20.3428548868364));
#169560=CARTESIAN_POINT('Ctrl Pts',(-16.6813498343758,-19.4710158172424,
20.3404840398845));
#169561=CARTESIAN_POINT('Ctrl Pts',(-16.6736061942495,-19.4393681863663,
20.3385839924498));
#169562=CARTESIAN_POINT('Ctrl Pts',(-16.6315963079364,-19.2487174569867,
20.3273754004952));
#169563=CARTESIAN_POINT('Ctrl Pts',(-16.6150140975621,-19.0863618491143,
20.3187785306604));
#169564=CARTESIAN_POINT('Ctrl Pts',(-16.6187513230299,-18.8068744552872,
20.3034766474504));
#169565=CARTESIAN_POINT('Ctrl Pts',(-16.6299804197431,-18.690399666584,
20.2969545227988));
#169566=CARTESIAN_POINT('Ctrl Pts',(-16.6532984925502,-18.5613922235532,
20.2892743737388));
#169567=CARTESIAN_POINT('Ctrl Pts',(-16.6559824485171,-18.5473566521685,
20.2884328726693));
#169568=CARTESIAN_POINT('Ctrl Pts',(-16.6604801968123,-18.5250619410746,
20.2870863059099));
#169569=CARTESIAN_POINT('Ctrl Pts',(-16.6622017631394,-18.5167844867783,
20.2865841814317));
#169570=CARTESIAN_POINT('Ctrl Pts',(-16.6653254436715,-18.5022041914738,
20.2856957812265));
#169571=CARTESIAN_POINT('Ctrl Pts',(-16.6667069045332,-18.495897001349,
20.2853101715272));
#169572=CARTESIAN_POINT('Ctrl Pts',(-16.6696238864007,-18.4828647905564,
20.2845106686236));
#169573=CARTESIAN_POINT('Ctrl Pts',(-16.6711634649905,-18.4761407653336,
20.2840966490654));
#169574=CARTESIAN_POINT('Ctrl Pts',(-16.6751997356624,-18.458900314784,
20.2830311571573));
#169575=CARTESIAN_POINT('Ctrl Pts',(-16.6777441326717,-18.4483953641108,
20.2823781553349));
#169576=CARTESIAN_POINT('Ctrl Pts',(-16.6886998490004,-18.4046306092178,
20.2796415923445));
#169577=CARTESIAN_POINT('Ctrl Pts',(-16.6978381947843,-18.3715597840504,
20.277534688551));
#169578=CARTESIAN_POINT('Ctrl Pts',(-16.7237400994648,-18.285981135677,
20.2719769974288));
#169579=CARTESIAN_POINT('Ctrl Pts',(-16.7417568792228,-18.2338826544624,
20.2684877683368));
#169580=CARTESIAN_POINT('Ctrl Pts',(-16.8015464442778,-18.080633104425,
20.2579141275802));
#169581=CARTESIAN_POINT('Ctrl Pts',(-16.8491461704739,-17.9819589765353,
20.2506813367646));
#169582=CARTESIAN_POINT('Ctrl Pts',(-16.9285139381713,-17.8455389585049,
20.2402556475015));
#169583=CARTESIAN_POINT('Ctrl Pts',(-16.954306752471,-17.8045122494924,
20.2370618076706));
#169584=CARTESIAN_POINT('Ctrl Pts',(-16.9913899411259,-17.7497891474341,
20.2327493449413));
#169585=CARTESIAN_POINT('Ctrl Pts',(-17.0014775419252,-17.7352967872106,
20.2316021016933));
#169586=CARTESIAN_POINT('Ctrl Pts',(-17.0427688014109,-17.6775306344351,
20.2270129848426));
#169587=CARTESIAN_POINT('Ctrl Pts',(-17.0754246199141,-17.6353132960956,
20.2236215821015));
#169588=CARTESIAN_POINT('Ctrl Pts',(-17.1152357822057,-17.587680591574,
20.2197920781617));
#169589=CARTESIAN_POINT('Ctrl Pts',(-17.1208693983504,-17.5810241763437,
20.2192568622761));
#169590=CARTESIAN_POINT('Ctrl Pts',(-17.1294614193724,-17.5709985365952,
20.2184508970899));
#169591=CARTESIAN_POINT('Ctrl Pts',(-17.1323895817939,-17.5676036810949,
20.2181780108231));
#169592=CARTESIAN_POINT('Ctrl Pts',(-17.1376648141155,-17.5615268159373,
20.2176896291212));
#169593=CARTESIAN_POINT('Ctrl Pts',(-17.1400078814604,-17.5588414204019,
20.217473845552));
#169594=CARTESIAN_POINT('Ctrl Pts',(-17.1451136751808,-17.5530194007646,
20.2170060997205));
#169595=CARTESIAN_POINT('Ctrl Pts',(-17.1478789038048,-17.549885047818,
20.2167543284641));
#169596=CARTESIAN_POINT('Ctrl Pts',(-17.1556717595684,-17.5411044967379,
20.216049077642));
#169597=CARTESIAN_POINT('Ctrl Pts',(-17.1607204333561,-17.535476945208,
20.2155971437204));
#169598=CARTESIAN_POINT('Ctrl Pts',(-17.1910710203988,-17.5020088162227,
20.2129089615556));
#169599=CARTESIAN_POINT('Ctrl Pts',(-17.2170829332868,-17.4748177921317,
20.2107230867002));
#169600=CARTESIAN_POINT('Ctrl Pts',(-17.3050419776655,-17.3876469742849,
20.2036512497106));
#169601=CARTESIAN_POINT('Ctrl Pts',(-17.3699313674244,-17.3307534011999,
20.1989284466934));
#169602=CARTESIAN_POINT('Ctrl Pts',(-17.5777740462778,-17.1698598044226,
20.1846244361364));
#169603=CARTESIAN_POINT('Ctrl Pts',(-17.7303956652488,-17.0796608677314,
20.1751347597826));
#169604=CARTESIAN_POINT('Ctrl Pts',(-17.9134594916861,-17.0003527365709,
20.1635408625699));
#169605=CARTESIAN_POINT('Ctrl Pts',(-17.9346252643696,-16.9915883752631,
20.1621987222171));
#169606=CARTESIAN_POINT('Ctrl Pts',(-17.9647938324817,-16.9796659155622,
20.1602816379588));
#169607=CARTESIAN_POINT('Ctrl Pts',(-17.9736826110846,-16.9762223474342,
20.1597163031272));
#169608=CARTESIAN_POINT('Ctrl Pts',(-17.9881703118271,-16.9707219653485,
20.1587939573545));
#169609=CARTESIAN_POINT('Ctrl Pts',(-17.9937552662259,-16.9686285503337,
20.1584381771129));
#169610=CARTESIAN_POINT('Ctrl Pts',(-18.0054702381554,-16.9642937876832,
20.1576914019823));
#169611=CARTESIAN_POINT('Ctrl Pts',(-18.0116019152963,-16.962057134963,
20.1573002549101));
#169612=CARTESIAN_POINT('Ctrl Pts',(-18.0262244633854,-16.9567997571908,
20.1563667515129));
#169613=CARTESIAN_POINT('Ctrl Pts',(-18.0347244213131,-16.9538048443001,
20.1558235435568));
#169614=CARTESIAN_POINT('Ctrl Pts',(-18.0634768852977,-16.9438799991201,
20.1539839864242));
#169615=CARTESIAN_POINT('Ctrl Pts',(-18.0838147826669,-16.9372031577252,
20.1526793179631));
#169616=CARTESIAN_POINT('Ctrl Pts',(-18.1954372001421,-16.9024240726618,
20.1454976501836));
#169617=CARTESIAN_POINT('Ctrl Pts',(-18.2884304783548,-16.8802193870545,
20.1394304838841));
#169618=CARTESIAN_POINT('Ctrl Pts',(-18.5505747220782,-16.8360933339181,
20.1221541194405));
#169619=CARTESIAN_POINT('Ctrl Pts',(-18.7213427941413,-16.8281961998806,
20.1106611848412));
#169620=CARTESIAN_POINT('Ctrl Pts',(-18.9278180397878,-16.843571348049,
20.0974473662598));
#169621=CARTESIAN_POINT('Ctrl Pts',(-18.964354763366,-16.8472496891824,
20.0951381494348));
#169622=CARTESIAN_POINT('Ctrl Pts',(-19.0078600839502,-16.8527761922972,
20.0924375781891));
#169623=CARTESIAN_POINT('Ctrl Pts',(-19.0149359624417,-16.8537114286337,
20.0919999066417));
#169624=CARTESIAN_POINT('Ctrl Pts',(-19.0264760932945,-16.8552961383495,
20.0912888007074));
#169625=CARTESIAN_POINT('Ctrl Pts',(-19.0309431718657,-16.8559241182242,
20.0910141988322));
#169626=CARTESIAN_POINT('Ctrl Pts',(-19.0389378162342,-16.8570740720078,
20.0905239744681));
#169627=CARTESIAN_POINT('Ctrl Pts',(-19.0424660887609,-16.8575906827378,
20.0903080542874));
#169628=CARTESIAN_POINT('Ctrl Pts',(-19.0501066447412,-16.8587291417745,
20.0898414121081));
#169629=CARTESIAN_POINT('Ctrl Pts',(-19.0542183931129,-16.8593541919041,
20.089590873572));
#169630=CARTESIAN_POINT('Ctrl Pts',(-19.065704759539,-16.8611349464289,
20.0888925480148));
#169631=CARTESIAN_POINT('Ctrl Pts',(-19.0730752303257,-16.8623175572134,
20.0884462582198));
#169632=CARTESIAN_POINT('Ctrl Pts',(-19.1159556285201,-16.8694306712002,
20.0858595223938));
#169633=CARTESIAN_POINT('Ctrl Pts',(-19.1513181919386,-16.8762276169945,
20.083765127398));
#169634=CARTESIAN_POINT('Ctrl Pts',(-19.2646840987895,-16.901031933425,
20.0771269191575));
#169635=CARTESIAN_POINT('Ctrl Pts',(-19.3418489569868,-16.9225623266271,
20.0727242248211));
#169636=CARTESIAN_POINT('Ctrl Pts',(-19.593408753145,-17.0083933092205,
20.0582339605817));
#169637=CARTESIAN_POINT('Ctrl Pts',(-19.7605250780659,-17.0912392324931,
20.0483000400703));
#169638=CARTESIAN_POINT('Ctrl Pts',(-19.9330199989337,-17.2071424343612,
20.0362131102457));
#169639=CARTESIAN_POINT('Ctrl Pts',(-19.9511593239992,-17.2197471292946,
20.0349182819175));
#169640=CARTESIAN_POINT('Ctrl Pts',(-19.9759653213987,-17.2375663780687,
20.0331128256876));
#169641=CARTESIAN_POINT('Ctrl Pts',(-19.9828033284739,-17.2425408027082,
20.0326114133183));
#169642=CARTESIAN_POINT('Ctrl Pts',(-19.9945041971574,-17.2511604714736,
20.0317469096588));
#169643=CARTESIAN_POINT('Ctrl Pts',(-19.9993815356592,-17.2547859590266,
20.0313845884453));
#169644=CARTESIAN_POINT('Ctrl Pts',(-20.0092368961525,-17.2621778718111,
20.0306484352683));
#169645=CARTESIAN_POINT('Ctrl Pts',(-20.0142140025671,-17.2659454123421,
20.0302745617791));
#169646=CARTESIAN_POINT('Ctrl Pts',(-20.0257427231244,-17.2747528325057,
20.0294035921968));
#169647=CARTESIAN_POINT('Ctrl Pts',(-20.0322815947566,-17.2798091552391,
20.0289058491875));
#169648=CARTESIAN_POINT('Ctrl Pts',(-20.0459650165516,-17.2905187939899,
20.0278562766694));
#169649=CARTESIAN_POINT('Ctrl Pts',(-20.0531030052954,-17.2961801849448,
20.0273041306485));
#169650=CARTESIAN_POINT('Ctrl Pts',(-20.0720088326311,-17.3113748974776,
20.0258292016242));
#169651=CARTESIAN_POINT('Ctrl Pts',(-20.0837111263355,-17.3209885898692,
20.0249032040786));
#169652=CARTESIAN_POINT('Ctrl Pts',(-20.1190845990346,-17.3506900790787,
20.02206357292));
#169653=CARTESIAN_POINT('Ctrl Pts',(-20.1424171217152,-17.3711730444877,
20.0201341054808));
#169654=CARTESIAN_POINT('Ctrl Pts',(-20.2894060406967,-17.5060483329457,
20.0076072380144));
#169655=CARTESIAN_POINT('Ctrl Pts',(-20.3994705267636,-17.63432960631,19.996420106974));
#169656=CARTESIAN_POINT('Ctrl Pts',(-20.5482438239332,-17.8565485344146,
19.9788036085486));
#169657=CARTESIAN_POINT('Ctrl Pts',(-20.5974983410433,-17.9426075318654,
19.9723513825577));
#169658=CARTESIAN_POINT('Ctrl Pts',(-20.6447646758537,-18.0405388980323,
19.9656328485742));
#169659=CARTESIAN_POINT('Ctrl Pts',(-20.648918712693,-18.0492988762204,
19.9650371755358));
#169660=CARTESIAN_POINT('Ctrl Pts',(-20.6549630923326,-18.0622746844772,
19.9641629690021));
#169661=CARTESIAN_POINT('Ctrl Pts',(-20.6568999800886,-18.066468517389,
19.9638816696384));
#169662=CARTESIAN_POINT('Ctrl Pts',(-20.6603117271959,-18.0739197560062,
19.96338413591));
#169663=CARTESIAN_POINT('Ctrl Pts',(-20.6617920753388,-18.0771745887519,
19.9631675666609));
#169664=CARTESIAN_POINT('Ctrl Pts',(-20.6649460104449,-18.0841560092352,
19.9627046797831));
#169665=CARTESIAN_POINT('Ctrl Pts',(-20.6666170550987,-18.0878836845945,
19.9624585183398));
#169666=CARTESIAN_POINT('Ctrl Pts',(-20.6711741824252,-18.0981288195111,
19.9617846298524));
#169667=CARTESIAN_POINT('Ctrl Pts',(-20.6740381863277,-18.1046561236399,
19.9613582347434));
#169668=CARTESIAN_POINT('Ctrl Pts',(-20.6891489338429,-18.139573026485,
19.9590923501057));
#169669=CARTESIAN_POINT('Ctrl Pts',(-20.70080629668,-18.1682154893823,19.9572865832381));
#169670=CARTESIAN_POINT('Ctrl Pts',(-20.7154850933187,-18.2066740726829,
19.9549187825041));
#169671=CARTESIAN_POINT('Ctrl Pts',(-20.7190678131875,-18.2162692972679,
19.9543326725714));
#169672=CARTESIAN_POINT('Ctrl Pts',(-20.7225805743325,-18.2258896093654,
19.9537493095993));
#169673=CARTESIAN_POINT('',(-20.8509996091575,-18.9532864007368,20.489056279057));
#169674=CARTESIAN_POINT('Ctrl Pts',(-20.7225805414791,-18.2258895193907,
19.7345260867578));
#169675=CARTESIAN_POINT('Ctrl Pts',(-20.6874528713457,-18.1296862512102,
19.7401269184544));
#169676=CARTESIAN_POINT('Ctrl Pts',(-20.6453764095337,-18.0361204043018,
19.7456315150547));
#169677=CARTESIAN_POINT('Ctrl Pts',(-20.5472452507785,-17.854436844477,
19.7569907277832));
#169678=CARTESIAN_POINT('Ctrl Pts',(-20.4911569404231,-17.7667157894665,
19.7628328457669));
#169679=CARTESIAN_POINT('Ctrl Pts',(-20.4204318628533,-17.6722210247135,
19.7697495964571));
#169680=CARTESIAN_POINT('Ctrl Pts',(-20.4118958804628,-17.6610499414193,
19.7705776882396));
#169681=CARTESIAN_POINT('Ctrl Pts',(-20.3980907440664,-17.6433513279784,
19.7719068005496));
#169682=CARTESIAN_POINT('Ctrl Pts',(-20.3928928721193,-17.6367685424178,
19.7724049994506));
#169683=CARTESIAN_POINT('Ctrl Pts',(-20.383631408929,-17.6251817134121,
19.7732888433485));
#169684=CARTESIAN_POINT('Ctrl Pts',(-20.3795838018406,-17.6201649874514,
19.7736738443173));
#169685=CARTESIAN_POINT('Ctrl Pts',(-20.3711396579048,-17.6097963221909,
19.7744744530363));
#169686=CARTESIAN_POINT('Ctrl Pts',(-20.3667396468177,-17.6044473234249,
19.7748901988436));
#169687=CARTESIAN_POINT('Ctrl Pts',(-20.3553245586717,-17.5907082312258,
19.7759651738961));
#169688=CARTESIAN_POINT('Ctrl Pts',(-20.3482706386027,-17.5823508103896,
19.7766259853985));
#169689=CARTESIAN_POINT('Ctrl Pts',(-20.31808827668,-17.5471480791616,19.7794392211317));
#169690=CARTESIAN_POINT('Ctrl Pts',(-20.2943536028448,-17.520832300646,
19.7816166541245));
#169691=CARTESIAN_POINT('Ctrl Pts',(-20.2303135476179,-17.4533153872665,
19.7874063674094));
#169692=CARTESIAN_POINT('Ctrl Pts',(-20.1889687607384,-17.4131449788479,
19.7910612098951));
#169693=CARTESIAN_POINT('Ctrl Pts',(-20.0462319705667,-17.2853622112502,
19.8033999413777));
#169694=CARTESIAN_POINT('Ctrl Pts',(-19.9381730377295,-17.205690623948,
19.8123263508122));
#169695=CARTESIAN_POINT('Ctrl Pts',(-19.7463729477041,-17.0905908192682,
19.8270271496118));
#169696=CARTESIAN_POINT('Ctrl Pts',(-19.6665527468826,-17.0493459947494,
19.8328476782571));
#169697=CARTESIAN_POINT('Ctrl Pts',(-19.575507996463,-17.0094124349534,
19.8389896805927));
#169698=CARTESIAN_POINT('Ctrl Pts',(-19.5666425075101,-17.0055959775086,
19.8395826821297));
#169699=CARTESIAN_POINT('Ctrl Pts',(-19.553503339794,-17.0000459692206,
19.8404537305182));
#169700=CARTESIAN_POINT('Ctrl Pts',(-19.5492497454052,-16.9982655974378,
19.8407345150701));
#169701=CARTESIAN_POINT('Ctrl Pts',(-19.5416882445545,-16.9951296724862,
19.8412314805884));
#169702=CARTESIAN_POINT('Ctrl Pts',(-19.5383826918266,-16.9937685875106,
19.8414479935852));
#169703=CARTESIAN_POINT('Ctrl Pts',(-19.5312874495523,-16.9908680682834,
19.841911139503));
#169704=CARTESIAN_POINT('Ctrl Pts',(-19.5274967521628,-16.9893312465497,
19.8421576142544));
#169705=CARTESIAN_POINT('Ctrl Pts',(-19.5170660144579,-16.9851375835843,
19.8428332436832));
#169706=CARTESIAN_POINT('Ctrl Pts',(-19.5104168572306,-16.9825033599321,
19.84326105494));
#169707=CARTESIAN_POINT('Ctrl Pts',(-19.4746420408568,-16.9685396355155,
19.8455480814061));
#169708=CARTESIAN_POINT('Ctrl Pts',(-19.4452799012861,-16.9578217767478,
19.8473728240998));
#169709=CARTESIAN_POINT('Ctrl Pts',(-19.2606291227351,-16.8950177553075,
19.8585873066993));
#169710=CARTESIAN_POINT('Ctrl Pts',(-19.0999558447015,-16.8604448758089,
19.8672421922195));
#169711=CARTESIAN_POINT('Ctrl Pts',(-18.8202504708911,-16.8335146080889,
19.8826237010964));
#169712=CARTESIAN_POINT('Ctrl Pts',(-18.702897242282,-16.8319889566493,
19.8891640627748));
#169713=CARTESIAN_POINT('Ctrl Pts',(-18.5717696808636,-16.8411767827914,
19.89686474355));
#169714=CARTESIAN_POINT('Ctrl Pts',(-18.557520965006,-16.8423202930212,
19.8977065146238));
#169715=CARTESIAN_POINT('Ctrl Pts',(-18.5348635405685,-16.8443697727556,
19.8990534368197));
#169716=CARTESIAN_POINT('Ctrl Pts',(-18.5264466389595,-16.8451819956567,
19.8995556443727));
#169717=CARTESIAN_POINT('Ctrl Pts',(-18.5116115646932,-16.8467033279711,
19.9004441463527));
#169718=CARTESIAN_POINT('Ctrl Pts',(-18.5051913110712,-16.8473914197982,
19.9008297743207));
#169719=CARTESIAN_POINT('Ctrl Pts',(-18.4919194257524,-16.8488752835143,
19.9016292707508));
#169720=CARTESIAN_POINT('Ctrl Pts',(-18.4850683420084,-16.8496751903146,
19.9020432653503));
#169721=CARTESIAN_POINT('Ctrl Pts',(-18.467494003228,-16.8518142143035,
19.9031085997143));
#169722=CARTESIAN_POINT('Ctrl Pts',(-18.4567769684261,-16.8532019714273,
19.9037614680075));
#169723=CARTESIAN_POINT('Ctrl Pts',(-18.4121029153976,-16.8593349870864,
19.9064966798583));
#169724=CARTESIAN_POINT('Ctrl Pts',(-18.3782546313789,-16.8648225743609,
19.9086023366605));
#169725=CARTESIAN_POINT('Ctrl Pts',(-18.2904311408629,-16.8812591230351,
19.9141559393124));
#169726=CARTESIAN_POINT('Ctrl Pts',(-18.2367261389649,-16.8934959314496,
19.9176422555395));
#169727=CARTESIAN_POINT('Ctrl Pts',(-18.0779620642814,-16.9362462346191,
19.9282103144687));
#169728=CARTESIAN_POINT('Ctrl Pts',(-17.9747308797145,-16.9728193735862,
19.9354404529297));
#169729=CARTESIAN_POINT('Ctrl Pts',(-17.8336085213,-17.03548881982,19.9456405414657));
#169730=CARTESIAN_POINT('Ctrl Pts',(-17.7930149545006,-17.0550900800902,
19.9486120582263));
#169731=CARTESIAN_POINT('Ctrl Pts',(-17.7315247515292,-17.0872416036616,
19.9531456726464));
#169732=CARTESIAN_POINT('Ctrl Pts',(-17.7101675392357,-17.0988816399811,
19.9547264897884));
#169733=CARTESIAN_POINT('Ctrl Pts',(-17.6764326838586,-17.118028982989,
19.9572285006724));
#169734=CARTESIAN_POINT('Ctrl Pts',(-17.6639235343898,-17.125299506022,
19.9581573866627));
#169735=CARTESIAN_POINT('Ctrl Pts',(-17.6195647019962,-17.1516936347483,
19.9614528844623));
#169736=CARTESIAN_POINT('Ctrl Pts',(-17.5881429798286,-17.1715278381798,
19.9637902390719));
#169737=CARTESIAN_POINT('Ctrl Pts',(-17.5513021557437,-17.1961622703615,
19.9665195003504));
#169738=CARTESIAN_POINT('Ctrl Pts',(-17.5453669772867,-17.2001747049735,
19.9669588353227));
#169739=CARTESIAN_POINT('Ctrl Pts',(-17.5357212599401,-17.2067672123169,
19.9676720954521));
#169740=CARTESIAN_POINT('Ctrl Pts',(-17.5319984685038,-17.2093291357115,
19.9679471997032));
#169741=CARTESIAN_POINT('Ctrl Pts',(-17.5253523535291,-17.2139342398943,
19.9684379640804));
#169742=CARTESIAN_POINT('Ctrl Pts',(-17.5224259733483,-17.2159728981589,
19.9686539247014));
#169743=CARTESIAN_POINT('Ctrl Pts',(-17.5161031271706,-17.2204014743542,
19.9691202496244));
#169744=CARTESIAN_POINT('Ctrl Pts',(-17.512708548118,-17.2227939865051,
19.9693704326359));
#169745=CARTESIAN_POINT('Ctrl Pts',(-17.5032547022296,-17.229498818016,
19.9700667645002));
#169746=CARTESIAN_POINT('Ctrl Pts',(-17.497211017662,-17.2338331493093,
19.9705114299368));
#169747=CARTESIAN_POINT('Ctrl Pts',(-17.4624098105271,-17.2590702037981,
19.9730698971643));
#169748=CARTESIAN_POINT('Ctrl Pts',(-17.4341577892071,-17.2806641666623,
19.9751388159078));
#169749=CARTESIAN_POINT('Ctrl Pts',(-17.3454026609008,-17.352115394916,
19.9816596593925));
#169750=CARTESIAN_POINT('Ctrl Pts',(-17.2871162323678,-17.4046271959472,
19.9859761467133));
#169751=CARTESIAN_POINT('Ctrl Pts',(-17.0992045780821,-17.593846606142,
20.0005222676099));
#169752=CARTESIAN_POINT('Ctrl Pts',(-16.9849636737446,-17.7445220969915,
20.0105785088926));
#169753=CARTESIAN_POINT('Ctrl Pts',(-16.8813887038695,-17.9273064227458,
20.022800862881));
#169754=CARTESIAN_POINT('Ctrl Pts',(-16.8709212628747,-17.9464637705268,
20.024080782655));
#169755=CARTESIAN_POINT('Ctrl Pts',(-16.8568320153054,-17.9732251689446,
20.0258686990049));
#169756=CARTESIAN_POINT('Ctrl Pts',(-16.8529562855613,-17.9806945104997,
20.0263677156111));
#169757=CARTESIAN_POINT('Ctrl Pts',(-16.8463633348376,-17.9935879683895,
20.0272291852752));
#169758=CARTESIAN_POINT('Ctrl Pts',(-16.8436246879338,-17.9990010596264,
20.0275908806638));
#169759=CARTESIAN_POINT('Ctrl Pts',(-16.8380199428566,-18.0101983784794,
20.0283391517862));
#169760=CARTESIAN_POINT('Ctrl Pts',(-16.8351569621256,-18.0159840880259,
20.0287258317863));
#169761=CARTESIAN_POINT('Ctrl Pts',(-16.8285446692681,-18.0295018568292,
20.0296294206712));
#169762=CARTESIAN_POINT('Ctrl Pts',(-16.8248159040004,-18.0372437888982,
20.0301470383833));
#169763=CARTESIAN_POINT('Ctrl Pts',(-16.8129860181424,-18.0621932751953,
20.0318156182407));
#169764=CARTESIAN_POINT('Ctrl Pts',(-16.8050697911191,-18.0794869982543,
20.0329729368148));
#169765=CARTESIAN_POINT('Ctrl Pts',(-16.7664422086887,-18.1669683439524,
20.0388325837442));
#169766=CARTESIAN_POINT('Ctrl Pts',(-16.7393271200857,-18.2386724539092,
20.043655426877));
#169767=CARTESIAN_POINT('Ctrl Pts',(-16.6828933440818,-18.4165126865405,
20.0556550719475));
#169768=CARTESIAN_POINT('Ctrl Pts',(-16.6578495633768,-18.5237698133059,
20.0629300907546));
#169769=CARTESIAN_POINT('Ctrl Pts',(-16.6304745517221,-18.7030651948591,
20.0749094501698));
#169770=CARTESIAN_POINT('Ctrl Pts',(-16.6232748135076,-18.7741571841864,
20.0796099927936));
#169771=CARTESIAN_POINT('Ctrl Pts',(-16.6173234463805,-18.8922862261699,
20.0872201671401));
#169772=CARTESIAN_POINT('Ctrl Pts',(-16.6165200639996,-18.9391617433935,
20.0901875453526));
#169773=CARTESIAN_POINT('Ctrl Pts',(-16.6173969601522,-18.993707969292,
20.093550872544));
#169774=CARTESIAN_POINT('Ctrl Pts',(-16.617562198295,-19.0013864213163,
20.0940222534842));
#169775=CARTESIAN_POINT('Ctrl Pts',(-16.6178938788572,-19.0136868803939,
20.0947738746448));
#169776=CARTESIAN_POINT('Ctrl Pts',(-16.6180336854372,-19.0183094542451,
20.0950555442425));
#169777=CARTESIAN_POINT('Ctrl Pts',(-16.6183087667263,-19.0265148275123,
20.0955540730967));
#169778=CARTESIAN_POINT('Ctrl Pts',(-16.6184379964238,-19.0300977836996,
20.0957712668605));
#169779=CARTESIAN_POINT('Ctrl Pts',(-16.6187320247361,-19.037712754986,
20.0962318134139));
#169780=CARTESIAN_POINT('Ctrl Pts',(-16.6188992490171,-19.0417446230268,
20.0964750290214));
#169781=CARTESIAN_POINT('Ctrl Pts',(-16.6193837843089,-19.0526723023102,
20.0971325791456));
#169782=CARTESIAN_POINT('Ctrl Pts',(-16.61972330015,-19.0595671491852,20.0975456874863));
#169783=CARTESIAN_POINT('Ctrl Pts',(-16.6216091496217,-19.0943958454679,
20.0996240509918));
#169784=CARTESIAN_POINT('Ctrl Pts',(-16.6236754513212,-19.122300181698,
20.1012618532593));
#169785=CARTESIAN_POINT('Ctrl Pts',(-16.6313320027011,-19.2037394886876,
20.1059829262815));
#169786=CARTESIAN_POINT('Ctrl Pts',(-16.6384114199252,-19.2571143661314,
20.1090026672967));
#169787=CARTESIAN_POINT('Ctrl Pts',(-16.6713309287523,-19.4488863426291,
20.1197625732026));
#169788=CARTESIAN_POINT('Ctrl Pts',(-16.7089186590469,-19.5848881569915,
20.1272454922137));
#169789=CARTESIAN_POINT('Ctrl Pts',(-16.7925855979229,-19.8010498797979,
20.1400721858099));
#169790=CARTESIAN_POINT('Ctrl Pts',(-16.8308817460597,-19.8837261216597,
20.1452182594085));
#169791=CARTESIAN_POINT('Ctrl Pts',(-16.8809429791038,-19.9757468040221,
20.1513597057753));
#169792=CARTESIAN_POINT('Ctrl Pts',(-16.8876272709988,-19.9877536259923,
20.1521693788542));
#169793=CARTESIAN_POINT('Ctrl Pts',(-16.8985329186672,-20.0069020791808,
20.1534744781851));
#169794=CARTESIAN_POINT('Ctrl Pts',(-16.9026802493365,-20.014085576193,
20.1539672431839));
#169795=CARTESIAN_POINT('Ctrl Pts',(-16.9101181252263,-20.026795456499,
20.15484481216));
#169796=CARTESIAN_POINT('Ctrl Pts',(-16.9133918572463,-20.0323315951911,
20.1552290023748));
#169797=CARTESIAN_POINT('Ctrl Pts',(-16.920264496237,-20.0438338097025,
20.1560313138591));
#169798=CARTESIAN_POINT('Ctrl Pts',(-16.9238677257642,-20.049797200572,
20.1564495900041));
#169799=CARTESIAN_POINT('Ctrl Pts',(-16.9332997739112,-20.0652346690286,
20.1575384654385));
#169800=CARTESIAN_POINT('Ctrl Pts',(-16.9391738857544,-20.0746806958294,
20.1582107256199));
#169801=CARTESIAN_POINT('Ctrl Pts',(-16.9649894067295,-20.1154735916245,
20.1611403459296));
#169802=CARTESIAN_POINT('Ctrl Pts',(-16.9856786284744,-20.1463372158215,
20.1634253634136));
#169803=CARTESIAN_POINT('Ctrl Pts',(-17.0427802356745,-20.2268547124876,
20.1695754983652));
#169804=CARTESIAN_POINT('Ctrl Pts',(-17.0805627792012,-20.27548897554,20.1734900625096));
#169805=CARTESIAN_POINT('Ctrl Pts',(-17.2176828067909,-20.4369418703856,
20.1871730860358));
#169806=CARTESIAN_POINT('Ctrl Pts',(-17.3268663024046,-20.5407855280383,
20.1972435375032));
#169807=CARTESIAN_POINT('Ctrl Pts',(-17.5000731974876,-20.6735503208341,
20.2114657080261));
#169808=CARTESIAN_POINT('Ctrl Pts',(-17.5559969615214,-20.7122902158823,
20.2158241259982));
#169809=CARTESIAN_POINT('Ctrl Pts',(-17.621585001016,-20.7531963703818,
20.2205966389122));
#169810=CARTESIAN_POINT('Ctrl Pts',(-17.6295087770583,-20.758066067549,
20.221167784964));
#169811=CARTESIAN_POINT('Ctrl Pts',(-17.6413497800566,-20.7652360923487,
20.2220129377211));
#169812=CARTESIAN_POINT('Ctrl Pts',(-17.6452426111969,-20.7675762112767,
20.2222894567441));
#169813=CARTESIAN_POINT('Ctrl Pts',(-17.652207156455,-20.7717323914563,
20.2227817516946));
#169814=CARTESIAN_POINT('Ctrl Pts',(-17.6552759503767,-20.7735532268517,
20.2229978359914));
#169815=CARTESIAN_POINT('Ctrl Pts',(-17.6619121768641,-20.7774681071625,
20.2234633060435));
#169816=CARTESIAN_POINT('Ctrl Pts',(-17.6654811363374,-20.7795594516879,
20.2237125165007));
#169817=CARTESIAN_POINT('Ctrl Pts',(-17.6754189477816,-20.7853437635344,
20.2244034058939));
#169818=CARTESIAN_POINT('Ctrl Pts',(-17.6818010391035,-20.7890140308966,
20.2248436388042));
#169819=CARTESIAN_POINT('Ctrl Pts',(-17.7180746128179,-20.8096234901797,
20.2273269816597));
#169820=CARTESIAN_POINT('Ctrl Pts',(-17.7483576777707,-20.8258673756419,
20.2293282352224));
#169821=CARTESIAN_POINT('Ctrl Pts',(-17.845167782707,-20.874799753902,20.235544061566));
#169822=CARTESIAN_POINT('Ctrl Pts',(-17.9130262181056,-20.9047379090595,
20.2396373940959));
#169823=CARTESIAN_POINT('Ctrl Pts',(-18.1646960184479,-21.0003264703336,
20.2543461995866));
#169824=CARTESIAN_POINT('Ctrl Pts',(-18.3557503211861,-21.0440493740088,
20.2647305712193));
#169825=CARTESIAN_POINT('Ctrl Pts',(-18.5710172382166,-21.0628213983424,
20.2773123779564));
#169826=CARTESIAN_POINT('Ctrl Pts',(-18.5919717205753,-21.064334792938,
20.2785448561205));
#169827=CARTESIAN_POINT('Ctrl Pts',(-18.6212107689498,-21.0660094940934,
20.2802766793572));
#169828=CARTESIAN_POINT('Ctrl Pts',(-18.6294794356704,-21.0664344398512,
20.2807677725091));
#169829=CARTESIAN_POINT('Ctrl Pts',(-18.6437752406276,-21.0670850734583,
20.2816192302153));
#169830=CARTESIAN_POINT('Ctrl Pts',(-18.649801282694,-21.0673335316246,
20.2819788777301));
#169831=CARTESIAN_POINT('Ctrl Pts',(-18.6623001742401,-21.067795377132,
20.2827264010955));
#169832=CARTESIAN_POINT('Ctrl Pts',(-18.6687730985218,-21.0680048187054,
20.2831143967306));
#169833=CARTESIAN_POINT('Ctrl Pts',(-18.6839663537912,-21.0684266401192,
20.2840271820159));
#169834=CARTESIAN_POINT('Ctrl Pts',(-18.6926871898646,-21.0686148296087,
20.2845527242529));
#169835=CARTESIAN_POINT('Ctrl Pts',(-18.7211448221247,-21.0690529860537,
20.286273041614));
#169836=CARTESIAN_POINT('Ctrl Pts',(-18.7408835413631,-21.0690808148962,
20.287474738067));
#169837=CARTESIAN_POINT('Ctrl Pts',(-18.8426899691093,-21.06780059505,20.2937180913376));
#169838=CARTESIAN_POINT('Ctrl Pts',(-18.9246215312924,-21.0619967595135,
20.2988987108291));
#169839=CARTESIAN_POINT('Ctrl Pts',(-19.1014577366167,-21.0390861545677,
20.3104043008588));
#169840=CARTESIAN_POINT('Ctrl Pts',(-19.1959536109683,-21.0202239775568,
20.316760858635));
#169841=CARTESIAN_POINT('Ctrl Pts',(-19.408567270004,-20.9624830253628,
20.3313187746994));
#169842=CARTESIAN_POINT('Ctrl Pts',(-19.5252266600362,-20.919498513639,
20.3394986164437));
#169843=CARTESIAN_POINT('Ctrl Pts',(-19.6459813842652,-20.8625150512887,
20.3477444034768));
#169844=CARTESIAN_POINT('Ctrl Pts',(-19.6544770805945,-20.8584364028467,
20.3483232252808));
#169845=CARTESIAN_POINT('Ctrl Pts',(-19.667048763378,-20.8522973076676,
20.3491774844709));
#169846=CARTESIAN_POINT('Ctrl Pts',(-19.6711456406842,-20.8502802483878,
20.3494555123114));
#169847=CARTESIAN_POINT('Ctrl Pts',(-19.6784341736302,-20.8466624607093,
20.3499494521817));
#169848=CARTESIAN_POINT('Ctrl Pts',(-19.6816283298214,-20.8450669025439,
20.3501656809456));
#169849=CARTESIAN_POINT('Ctrl Pts',(-19.6884253704846,-20.8416501022892,
20.3506252931843));
#169850=CARTESIAN_POINT('Ctrl Pts',(-19.6920270743343,-20.8398266399154,
20.350868534611));
#169851=CARTESIAN_POINT('Ctrl Pts',(-19.7018628016953,-20.8348116329862,
20.3515320190684));
#169852=CARTESIAN_POINT('Ctrl Pts',(-19.708086303349,-20.8315994054487,
20.3519509839734));
#169853=CARTESIAN_POINT('Ctrl Pts',(-19.7219629531984,-20.8243496126087,
20.3528835050296));
#169854=CARTESIAN_POINT('Ctrl Pts',(-19.7296075627843,-20.8202958692774,
20.353396097376));
#169855=CARTESIAN_POINT('Ctrl Pts',(-19.7531083550483,-20.8076487849892,
20.3549690551881));
#169856=CARTESIAN_POINT('Ctrl Pts',(-19.7688801489266,-20.7988993946727,
20.3560206888475));
#169857=CARTESIAN_POINT('Ctrl Pts',(-19.8292097129774,-20.7644161006235,
20.3600352851188));
#169858=CARTESIAN_POINT('Ctrl Pts',(-19.8729380917612,-20.7372610939267,
20.3629281934109));
#169859=CARTESIAN_POINT('Ctrl Pts',(-20.029494426291,-20.6319444752037,
20.3733821140651));
#169860=CARTESIAN_POINT('Ctrl Pts',(-20.1356376904219,-20.5444614472474,
20.3806823136807));
#169861=CARTESIAN_POINT('Ctrl Pts',(-20.3014488632376,-20.3782896964381,
20.3936323161404));
#169862=CARTESIAN_POINT('Ctrl Pts',(-20.3654679332443,-20.3045927518625,
20.3991276302478));
#169863=CARTESIAN_POINT('Ctrl Pts',(-20.4325704368393,-20.2156224953328,
20.4056590619318));
#169864=CARTESIAN_POINT('Ctrl Pts',(-20.4408544633794,-20.2044101431239,
20.4064802772414));
#169865=CARTESIAN_POINT('Ctrl Pts',(-20.453924079103,-20.1863500052783,
20.4078004313522));
#169866=CARTESIAN_POINT('Ctrl Pts',(-20.4587810067739,-20.179554173562,
20.4082966089618));
#169867=CARTESIAN_POINT('Ctrl Pts',(-20.4673114115778,-20.1674678244488,
20.4091781163726));
#169868=CARTESIAN_POINT('Ctrl Pts',(-20.4710012225956,-20.1621889245329,
20.4095628134441));
#169869=CARTESIAN_POINT('Ctrl Pts',(-20.4786175055421,-20.1511859492998,
20.4103640381269));
#169870=CARTESIAN_POINT('Ctrl Pts',(-20.4825400239823,-20.1454592428685,
20.4107807099763));
#169871=CARTESIAN_POINT('Ctrl Pts',(-20.4926083156445,-20.1306037909207,
20.4118607634172));
#169872=CARTESIAN_POINT('Ctrl Pts',(-20.4987111411793,-20.1214463155108,
20.4125257557873));
#169873=CARTESIAN_POINT('Ctrl Pts',(-20.5245008363533,-20.0820865016081,
20.4153809048838));
#169874=CARTESIAN_POINT('Ctrl Pts',(-20.5434849140851,-20.0514329633956,
20.4175970072924));
#169875=CARTESIAN_POINT('Ctrl Pts',(-20.5914634161642,-19.9693509097231,
20.4235153408445));
#169876=CARTESIAN_POINT('Ctrl Pts',(-20.6191038822203,-19.9171712668829,
20.4272625224157));
#169877=CARTESIAN_POINT('Ctrl Pts',(-20.7103212337429,-19.7260631148771,
20.4409158349975));
#169878=CARTESIAN_POINT('Ctrl Pts',(-20.761002043115,-19.5815043387839,
20.4511527917293));
#169879=CARTESIAN_POINT('Ctrl Pts',(-20.8019773180527,-19.4057911539328,
20.4629187022516));
#169880=CARTESIAN_POINT('Ctrl Pts',(-20.8077392224272,-19.378687636761,
20.4647138326753));
#169881=CARTESIAN_POINT('Ctrl Pts',(-20.8211288655409,-19.3090051099935,
20.4692668387034));
#169882=CARTESIAN_POINT('Ctrl Pts',(-20.8279872927794,-19.2662886519038,
20.4719989986381));
#169883=CARTESIAN_POINT('Ctrl Pts',(-20.8344943174084,-19.2159486775211,
20.4751271999216));
#169884=CARTESIAN_POINT('Ctrl Pts',(-20.8354165124151,-19.208503269007,
20.4755875273787));
#169885=CARTESIAN_POINT('Ctrl Pts',(-20.8368427989704,-19.1964637388768,
20.4763279424358));
#169886=CARTESIAN_POINT('Ctrl Pts',(-20.8373714508299,-19.1918726695058,
20.4766093594304));
#169887=CARTESIAN_POINT('Ctrl Pts',(-20.8382824835703,-19.1837261659555,
20.4771070231343));
#169888=CARTESIAN_POINT('Ctrl Pts',(-20.8386708939738,-19.180171460507,
20.4773236053863));
#169889=CARTESIAN_POINT('Ctrl Pts',(-20.8394063448191,-19.1732789727038,
20.4777424356568));
#169890=CARTESIAN_POINT('Ctrl Pts',(-20.8397544539967,-19.1699413691777,
20.4779447451182));
#169891=CARTESIAN_POINT('Ctrl Pts',(-20.8405037112363,-19.1625882231517,
20.4783893752405));
#169892=CARTESIAN_POINT('Ctrl Pts',(-20.8409013174799,-19.1585723219416,
20.4786314984297));
#169893=CARTESIAN_POINT('Ctrl Pts',(-20.8418560162692,-19.148640095738,
20.4792286215703));
#169894=CARTESIAN_POINT('Ctrl Pts',(-20.842399689828,-19.14272247474,20.4795828954843));
#169895=CARTESIAN_POINT('Ctrl Pts',(-20.844583901369,-19.117796825005,20.48106914855));
#169896=CARTESIAN_POINT('Ctrl Pts',(-20.8459924221905,-19.0987687150597,
20.4821890985016));
#169897=CARTESIAN_POINT('Ctrl Pts',(-20.8496863090821,-19.0376545415139,
20.4857465687598));
#169898=CARTESIAN_POINT('Ctrl Pts',(-20.8509723412701,-18.9955169026794,
20.4881393720512));
#169899=CARTESIAN_POINT('Ctrl Pts',(-20.8509995586429,-18.9533670061129,
20.490497217366));
#169900=CARTESIAN_POINT('Ctrl Pts',(-20.7225805737622,-18.2258896078036,
20.5336910569984));
#169901=CARTESIAN_POINT('Ctrl Pts',(-20.7472974566424,-18.2935811236775,
20.5293719648838));
#169902=CARTESIAN_POINT('Ctrl Pts',(-20.7685452928513,-18.3625125368533,
20.5250528727692));
#169903=CARTESIAN_POINT('Ctrl Pts',(-20.7862157788573,-18.4322891217137,
20.5207337806546));
#169904=CARTESIAN_POINT('Ctrl Pts',(-20.803893991431,-18.502096216969,20.5164127999808));
#169905=CARTESIAN_POINT('Ctrl Pts',(-20.8179916434005,-18.5727487327075,
20.5120918193071));
#169906=CARTESIAN_POINT('Ctrl Pts',(-20.8284516637963,-18.6438422027255,
20.5077708386333));
#169907=CARTESIAN_POINT('Ctrl Pts',(-20.8389271742135,-18.7150409535491,
20.5034434591113));
#169908=CARTESIAN_POINT('Ctrl Pts',(-20.8457542576745,-18.7866814680688,
20.4991160795893));
#169909=CARTESIAN_POINT('Ctrl Pts',(-20.8489278328486,-18.8583556630536,
20.4947887000673));
#169910=CARTESIAN_POINT('Ctrl Pts',(-20.8503291635241,-18.8900042746542,
20.4928778930639));
#169911=CARTESIAN_POINT('Ctrl Pts',(-20.8510188273478,-18.9216594744888,
20.4909670860604));
#169912=CARTESIAN_POINT('Ctrl Pts',(-20.8509996091575,-18.9532864007368,
20.489056279057));
#169913=CARTESIAN_POINT('Origin',(-18.734,-18.952,0.));
#169914=CARTESIAN_POINT('',(-20.7225805737622,-18.2258896078036,21.5555703780636));
#169915=CARTESIAN_POINT('',(-20.7225805737622,-18.2258896078036,21.3335535462005));
#169916=CARTESIAN_POINT('',(-20.7225805737622,-18.2258896078036,0.));
#169917=CARTESIAN_POINT('',(-20.8509993841958,-18.953614718169,21.5109437210328));
#169918=CARTESIAN_POINT('Ctrl Pts',(-20.8509993841958,-18.953614718169,
21.5109437210328));
#169919=CARTESIAN_POINT('Ctrl Pts',(-20.8510540300824,-18.8819704457194,
21.5152671815625));
#169920=CARTESIAN_POINT('Ctrl Pts',(-20.8474675421558,-18.8101916547056,
21.5195906420923));
#169921=CARTESIAN_POINT('Ctrl Pts',(-20.840225458876,-18.7386849363444,
21.523914102622));
#169922=CARTESIAN_POINT('Ctrl Pts',(-20.83299097412,-18.6672532441145,21.5282330268994));
#169923=CARTESIAN_POINT('Ctrl Pts',(-20.8221085457459,-18.5960935495738,
21.5325519511768));
#169924=CARTESIAN_POINT('Ctrl Pts',(-20.807615734365,-18.525611930052,21.5368708754542));
#169925=CARTESIAN_POINT('Ctrl Pts',(-20.7931333503066,-18.4551810208142,
21.5411866923416));
#169926=CARTESIAN_POINT('Ctrl Pts',(-20.7750458352844,-18.3854277039634,
21.5455025092291));
#169927=CARTESIAN_POINT('Ctrl Pts',(-20.7534422763024,-18.316750527208,
21.5498183261165));
#169928=CARTESIAN_POINT('Ctrl Pts',(-20.7438446499629,-18.2862399117533,
21.5517356767656));
#169929=CARTESIAN_POINT('Ctrl Pts',(-20.7335537446294,-18.2559415594814,
21.5536530274146));
#169930=CARTESIAN_POINT('Ctrl Pts',(-20.7225805737622,-18.2258896078036,
21.5555703780636));
#169931=CARTESIAN_POINT('Ctrl Pts',(-20.8509994311328,-18.953551961105,
21.509989519712));
#169932=CARTESIAN_POINT('Ctrl Pts',(-20.8509485267258,-19.022989655363,
21.5054226551334));
#169933=CARTESIAN_POINT('Ctrl Pts',(-20.8474812907043,-19.0923897728265,
21.500900987759));
#169934=CARTESIAN_POINT('Ctrl Pts',(-20.8382974849423,-19.1847367233776,
21.4950377275334));
#169935=CARTESIAN_POINT('Ctrl Pts',(-20.8356021939193,-19.2079347726058,
21.4935780223835));
#169936=CARTESIAN_POINT('Ctrl Pts',(-20.8317147194992,-19.2371659041953,
21.4917592813289));
#169937=CARTESIAN_POINT('Ctrl Pts',(-20.8308795084294,-19.2432438265875,
21.4913822453896));
#169938=CARTESIAN_POINT('Ctrl Pts',(-20.8294396375592,-19.25339455379,21.4907545413536));
#169939=CARTESIAN_POINT('Ctrl Pts',(-20.8288495023032,-19.2574693357115,
21.4905030984012));
#169940=CARTESIAN_POINT('Ctrl Pts',(-20.8277537589393,-19.2648827230509,
21.4900466455369));
#169941=CARTESIAN_POINT('Ctrl Pts',(-20.8272520454091,-19.2682218781408,
21.4898414207734));
#169942=CARTESIAN_POINT('Ctrl Pts',(-20.8262054097198,-19.2750761148474,
21.4894209425127));
#169943=CARTESIAN_POINT('Ctrl Pts',(-20.8256596197261,-19.2785910105254,
21.489205745317));
#169944=CARTESIAN_POINT('Ctrl Pts',(-20.8244066869482,-19.286527930997,
21.4887207763407));
#169945=CARTESIAN_POINT('Ctrl Pts',(-20.8236943731061,-19.2909490836633,
21.4884513018776));
#169946=CARTESIAN_POINT('Ctrl Pts',(-20.8214990062823,-19.3043051658924,
21.4876391708809));
#169947=CARTESIAN_POINT('Ctrl Pts',(-20.8199726159162,-19.313233004385,
21.4870989280484));
#169948=CARTESIAN_POINT('Ctrl Pts',(-20.8078182965081,-19.3816762404416,
21.4829755341491));
#169949=CARTESIAN_POINT('Ctrl Pts',(-20.7947015599908,-19.4407274473077,
21.4795238028164));
#169950=CARTESIAN_POINT('Ctrl Pts',(-20.7741842858873,-19.517415715384,
21.4750859567501));
#169951=CARTESIAN_POINT('Ctrl Pts',(-20.7690503570717,-19.5356239562734,
21.4740356752781));
#169952=CARTESIAN_POINT('Ctrl Pts',(-20.752036519566,-19.5930097141763,
21.4707296572627));
#169953=CARTESIAN_POINT('Ctrl Pts',(-20.7392637897188,-19.6319133317566,
21.4684943567092));
#169954=CARTESIAN_POINT('Ctrl Pts',(-20.7134200740027,-19.703548601181,
21.4643516799029));
#169955=CARTESIAN_POINT('Ctrl Pts',(-20.700644664369,-19.7363710280158,
21.4624428384245));
#169956=CARTESIAN_POINT('Ctrl Pts',(-20.6589738879128,-19.8360030588782,
21.45657927303));
#169957=CARTESIAN_POINT('Ctrl Pts',(-20.6274484736872,-19.9016515661354,
21.4526164834016));
#169958=CARTESIAN_POINT('Ctrl Pts',(-20.5661674190936,-20.0140269091526,
21.4455035225684));
#169959=CARTESIAN_POINT('Ctrl Pts',(-20.5378432111702,-20.0614537505821,
21.4423911736075));
#169960=CARTESIAN_POINT('Ctrl Pts',(-20.4889701482696,-20.1364600956493,
21.4372424305058));
#169961=CARTESIAN_POINT('Ctrl Pts',(-20.4695463826916,-20.1647425511322,
21.4352459081717));
#169962=CARTESIAN_POINT('Ctrl Pts',(-20.4431384531694,-20.2012600073017,
21.4325885793575));
#169963=CARTESIAN_POINT('Ctrl Pts',(-20.4367657948285,-20.2099322157393,
21.4319514664983));
#169964=CARTESIAN_POINT('Ctrl Pts',(-20.4262255532679,-20.2240490093817,
21.4309042295645));
#169965=CARTESIAN_POINT('Ctrl Pts',(-20.4220971023159,-20.2295226717532,
21.4304956466839));
#169966=CARTESIAN_POINT('Ctrl Pts',(-20.4140583306678,-20.2400737850873,
21.4297031032962));
#169967=CARTESIAN_POINT('Ctrl Pts',(-20.410151395252,-20.2451537298637,
21.4293192798396));
#169968=CARTESIAN_POINT('Ctrl Pts',(-20.4010835076038,-20.2568340039861,
21.4284315172956));
#169969=CARTESIAN_POINT('Ctrl Pts',(-20.3959063430362,-20.2634215581138,
21.4279269323589));
#169970=CARTESIAN_POINT('Ctrl Pts',(-20.381893156061,-20.2810360464795,
21.426567108629));
#169971=CARTESIAN_POINT('Ctrl Pts',(-20.3729857267863,-20.2920053875725,
21.4257089935978));
#169972=CARTESIAN_POINT('Ctrl Pts',(-20.2682886291546,-20.4183322891219,
21.4156928769048));
#169973=CARTESIAN_POINT('Ctrl Pts',(-20.1606324264817,-20.5232656833021,
21.4060183990526));
#169974=CARTESIAN_POINT('Ctrl Pts',(-19.9681077757239,-20.6747021725785,
21.3898620876248));
#169975=CARTESIAN_POINT('Ctrl Pts',(-19.8895203929384,-20.7283721356634,
21.3835369424866));
#169976=CARTESIAN_POINT('Ctrl Pts',(-19.7687964020942,-20.799406702276,
21.3744151972906));
#169977=CARTESIAN_POINT('Ctrl Pts',(-19.7292807463733,-20.8209922089922,
21.3715174048873));
#169978=CARTESIAN_POINT('Ctrl Pts',(-19.667082796194,-20.852435315658,21.3671222453147));
#169979=CARTESIAN_POINT('Ctrl Pts',(-19.6448669637259,-20.8631827207263,
21.3655841186835));
#169980=CARTESIAN_POINT('Ctrl Pts',(-19.6165112336334,-20.8762936314066,
21.3636654433987));
#169981=CARTESIAN_POINT('Ctrl Pts',(-19.6105424043741,-20.8790198424845,
21.3632640343944));
#169982=CARTESIAN_POINT('Ctrl Pts',(-19.6014988122009,-20.8830997114459,
21.3626596782316));
#169983=CARTESIAN_POINT('Ctrl Pts',(-19.5984334106001,-20.8844738455462,
21.3624554896844));
#169984=CARTESIAN_POINT('Ctrl Pts',(-19.5921218303903,-20.8872851280853,
21.3620364532144));
#169985=CARTESIAN_POINT('Ctrl Pts',(-19.5888753552478,-20.8887213867573,
21.3618216677972));
#169986=CARTESIAN_POINT('Ctrl Pts',(-19.5815844043418,-20.8919250393223,
21.3613409679369));
#169987=CARTESIAN_POINT('Ctrl Pts',(-19.5775380097716,-20.8936879531881,
21.361075329669));
#169988=CARTESIAN_POINT('Ctrl Pts',(-19.5672267492065,-20.8981419974324,
21.3604012509681));
#169989=CARTESIAN_POINT('Ctrl Pts',(-19.5609542871364,-20.9008155632606,
21.3599938570443));
#169990=CARTESIAN_POINT('Ctrl Pts',(-19.525258987277,-20.9158269091106,
21.3576899172704));
#169991=CARTESIAN_POINT('Ctrl Pts',(-19.4955714171562,-20.9275293307902,
21.3558293488611));
#169992=CARTESIAN_POINT('Ctrl Pts',(-19.2794561049982,-21.0071224262951,
21.342605264977));
#169993=CARTESIAN_POINT('Ctrl Pts',(-19.084552194699,-21.0491845593995,
21.3322948172777));
#169994=CARTESIAN_POINT('Ctrl Pts',(-18.8308771116841,-21.0675206426042,
21.3181607866529));
#169995=CARTESIAN_POINT('Ctrl Pts',(-18.774997640159,-21.0693406171215,
21.3150108687555));
#169996=CARTESIAN_POINT('Ctrl Pts',(-18.6844306692982,-21.0687037816697,
21.3098016289188));
#169997=CARTESIAN_POINT('Ctrl Pts',(-18.6497597955011,-21.0676075730561,
21.3077829067633));
#169998=CARTESIAN_POINT('Ctrl Pts',(-18.6042813203144,-21.0650499740806,
21.3050966179787));
#169999=CARTESIAN_POINT('Ctrl Pts',(-18.593434775635,-21.0643561583848,
21.3044530871149));
#170000=CARTESIAN_POINT('Ctrl Pts',(-18.5756893554948,-21.063083764776,
21.3033953861573));
#170001=CARTESIAN_POINT('Ctrl Pts',(-18.5687870400536,-21.062554808145,
21.3029827754469));
#170002=CARTESIAN_POINT('Ctrl Pts',(-18.5554387656461,-21.0614659865788,
21.3021824555244));
#170003=CARTESIAN_POINT('Ctrl Pts',(-18.5489925275103,-21.0609104050745,
21.3017948850868));
#170004=CARTESIAN_POINT('Ctrl Pts',(-18.5341249892073,-21.0595603263143,
21.3008984733759));
#170005=CARTESIAN_POINT('Ctrl Pts',(-18.5257057434526,-21.0587448940124,
21.3003889799265));
#170006=CARTESIAN_POINT('Ctrl Pts',(-18.5030993884878,-21.0564185568567,
21.2990158239832));
#170007=CARTESIAN_POINT('Ctrl Pts',(-18.4889224797778,-21.0548146728429,
21.2981492569185));
#170008=CARTESIAN_POINT('Ctrl Pts',(-18.3611878658061,-21.0390543419627,
21.2902911432454));
#170009=CARTESIAN_POINT('Ctrl Pts',(-18.2489541415696,-21.015857531346,
21.2830116140944));
#170010=CARTESIAN_POINT('Ctrl Pts',(-17.9820874112819,-20.9377247165375,
21.2648714388788));
#170011=CARTESIAN_POINT('Ctrl Pts',(-17.8308835810645,-20.8736804146279,
21.2538542156912));
#170012=CARTESIAN_POINT('Ctrl Pts',(-17.6600660801652,-20.7766723789927,
21.2413718810939));
#170013=CARTESIAN_POINT('Ctrl Pts',(-17.6319421012103,-20.75982521716,21.2393174949565));
#170014=CARTESIAN_POINT('Ctrl Pts',(-17.5980639138651,-20.7384465231899,
21.2368541846157));
#170015=CARTESIAN_POINT('Ctrl Pts',(-17.5919287755815,-20.7345305870816,
21.2364085626905));
#170016=CARTESIAN_POINT('Ctrl Pts',(-17.5823450909889,-20.7283437216201,
21.2357133475665));
#170017=CARTESIAN_POINT('Ctrl Pts',(-17.5788828526622,-20.7260942543688,
21.2354623748231));
#170018=CARTESIAN_POINT('Ctrl Pts',(-17.5724302582162,-20.7218750116092,
21.2349950117687));
#170019=CARTESIAN_POINT('Ctrl Pts',(-17.5694383446513,-20.7199077953743,
21.2347784624356));
#170020=CARTESIAN_POINT('Ctrl Pts',(-17.5626252435353,-20.7154033056093,
21.2342856861504));
#170021=CARTESIAN_POINT('Ctrl Pts',(-17.5588073113675,-20.7128612051516,
21.2340097869724));
#170022=CARTESIAN_POINT('Ctrl Pts',(-17.5471006926868,-20.705011532934,
21.2331644701471));
#170023=CARTESIAN_POINT('Ctrl Pts',(-17.5392393508416,-20.6996631251867,
21.2325977265799));
#170024=CARTESIAN_POINT('Ctrl Pts',(-17.4690650479913,-20.6512257302489,
21.2275443409458));
#170025=CARTESIAN_POINT('Ctrl Pts',(-17.4090637257419,-20.6048687098913,
21.2232630108996));
#170026=CARTESIAN_POINT('Ctrl Pts',(-17.2444652312138,-20.4629635446243,
21.2112324759176));
#170027=CARTESIAN_POINT('Ctrl Pts',(-17.1467977966924,-20.360018520536,
21.2037083659344));
#170028=CARTESIAN_POINT('Ctrl Pts',(-17.0222841640855,-20.1992127960163,
21.192456219598));
#170029=CARTESIAN_POINT('Ctrl Pts',(-16.9865970645232,-20.1487008749523,
21.1889869145585));
#170030=CARTESIAN_POINT('Ctrl Pts',(-16.9330236535886,-20.065356093378,
21.183300741611));
#170031=CARTESIAN_POINT('Ctrl Pts',(-16.9137065451066,-20.0334846644639,
21.1811350177436));
#170032=CARTESIAN_POINT('Ctrl Pts',(-16.8897212650156,-19.9914464986765,
21.1782819047434));
#170033=CARTESIAN_POINT('Ctrl Pts',(-16.8842776702087,-19.981728299811,
21.1776225832733));
#170034=CARTESIAN_POINT('Ctrl Pts',(-16.8755514268846,-19.9658572515203,
21.1765460343363));
#170035=CARTESIAN_POINT('Ctrl Pts',(-16.8722219963749,-19.9597302658975,
21.1761304847091));
#170036=CARTESIAN_POINT('Ctrl Pts',(-16.8658787582937,-19.9479183834283,
21.1753294144832));
#170037=CARTESIAN_POINT('Ctrl Pts',(-16.8628604741948,-19.9422359687051,
21.1749440587556));
#170038=CARTESIAN_POINT('Ctrl Pts',(-16.8560107188025,-19.9291970413597,
21.1740598207672));
#170039=CARTESIAN_POINT('Ctrl Pts',(-16.8521965013089,-19.9218316282696,
21.1735603356746));
#170040=CARTESIAN_POINT('Ctrl Pts',(-16.8421821529314,-19.9022119969455,
21.1722297439669));
#170041=CARTESIAN_POINT('Ctrl Pts',(-16.8360578920201,-19.8899196908249,
21.1713959949471));
#170042=CARTESIAN_POINT('Ctrl Pts',(-16.790517079691,-19.7962397296996,
21.1650403130209));
#170043=CARTESIAN_POINT('Ctrl Pts',(-16.7562372080106,-19.7124716821331,
21.1593415150642));
#170044=CARTESIAN_POINT('Ctrl Pts',(-16.6828132220643,-19.4941315697377,
21.1444672100533));
#170045=CARTESIAN_POINT('Ctrl Pts',(-16.6514713629923,-19.3573928277871,
21.1351153440828));
#170046=CARTESIAN_POINT('Ctrl Pts',(-16.6269164194993,-19.1639450369983,
21.1223445127553));
#170047=CARTESIAN_POINT('Ctrl Pts',(-16.6221156279491,-19.1090577748662,
21.1187756336227));
#170048=CARTESIAN_POINT('Ctrl Pts',(-16.6180913201353,-19.0256653698077,
21.113491487971));
#170049=CARTESIAN_POINT('Ctrl Pts',(-16.6172932042516,-18.9972620455094,
21.1117160264734));
#170050=CARTESIAN_POINT('Ctrl Pts',(-16.617011841326,-18.9619126873634,
21.1095435982719));
#170051=CARTESIAN_POINT('Ctrl Pts',(-16.6169907237174,-18.9549753233616,
21.1091190403129));
#170052=CARTESIAN_POINT('Ctrl Pts',(-16.6170112736636,-18.9439953278897,
21.108450035994));
#170053=CARTESIAN_POINT('Ctrl Pts',(-16.6170304189174,-18.939952775636,
21.1082043603217));
#170054=CARTESIAN_POINT('Ctrl Pts',(-16.6170883626996,-18.9323290679206,
21.1077422775837));
#170055=CARTESIAN_POINT('Ctrl Pts',(-16.6171246681997,-18.9287479998222,
21.1075257396181));
#170056=CARTESIAN_POINT('Ctrl Pts',(-16.6172284559512,-18.9205602942581,
21.1070318079626));
#170057=CARTESIAN_POINT('Ctrl Pts',(-16.617301888378,-18.9159537801199,
21.106754750254));
#170058=CARTESIAN_POINT('Ctrl Pts',(-16.6175368217481,-18.9037217612884,
21.1060211892931));
#170059=CARTESIAN_POINT('Ctrl Pts',(-16.6177244972546,-18.8960967471679,
21.1055661123605));
#170060=CARTESIAN_POINT('Ctrl Pts',(-16.619329749684,-18.8426269241492,
21.1023893126151));
#170061=CARTESIAN_POINT('Ctrl Pts',(-16.6221958022221,-18.7968341408434,
21.0997427792956));
#170062=CARTESIAN_POINT('Ctrl Pts',(-16.630125607129,-18.7136222305225,
21.0950110828089));
#170063=CARTESIAN_POINT('Ctrl Pts',(-16.634706330537,-18.6761780606287,
21.0929106702665));
#170064=CARTESIAN_POINT('Ctrl Pts',(-16.6596435950099,-18.5094347611808,
21.0836107017199));
#170065=CARTESIAN_POINT('Ctrl Pts',(-16.6909636048286,-18.3820682065839,
21.0766335490723));
#170066=CARTESIAN_POINT('Ctrl Pts',(-16.7627868872662,-18.1749472393378,
21.0645331902965));
#170067=CARTESIAN_POINT('Ctrl Pts',(-16.7969204146279,-18.0933893530314,
21.059561163438));
#170068=CARTESIAN_POINT('Ctrl Pts',(-16.845136893778,-17.9958062862303,
21.0532176623386));
#170069=CARTESIAN_POINT('Ctrl Pts',(-16.8544957140584,-17.977539201562,
21.0520126536466));
#170070=CARTESIAN_POINT('Ctrl Pts',(-16.8682708154767,-17.9515890626519,
21.0502743160111));
#170071=CARTESIAN_POINT('Ctrl Pts',(-16.8724722134385,-17.9437928140642,
21.0497485918527));
#170072=CARTESIAN_POINT('Ctrl Pts',(-16.879839066429,-17.9303256837383,
21.0488343255088));
#170073=CARTESIAN_POINT('Ctrl Pts',(-16.8829819479648,-17.9246425424038,
21.0484465936424));
#170074=CARTESIAN_POINT('Ctrl Pts',(-16.8890742005738,-17.9137448849469,
21.0476993804587));
#170075=CARTESIAN_POINT('Ctrl Pts',(-16.8920196575953,-17.9085282436169,
21.0473400426678));
#170076=CARTESIAN_POINT('Ctrl Pts',(-16.8997915891383,-17.8948989772083,
21.0463968450716));
#170077=CARTESIAN_POINT('Ctrl Pts',(-16.9046537624411,-17.8865069661934,
21.0458116978628));
#170078=CARTESIAN_POINT('Ctrl Pts',(-16.9217171616442,-17.8575169915387,
21.0437748597726));
#170079=CARTESIAN_POINT('Ctrl Pts',(-16.9342096439647,-17.8370933929544,
21.0423125956436));
#170080=CARTESIAN_POINT('Ctrl Pts',(-17.0303083072501,-17.6858098651131,
21.0312706867671));
#170081=CARTESIAN_POINT('Ctrl Pts',(-17.1277255615655,-17.5643153454577,
21.0211549202071));
#170082=CARTESIAN_POINT('Ctrl Pts',(-17.2901100872525,-17.4020330559754,
21.0059879943424));
#170083=CARTESIAN_POINT('Ctrl Pts',(-17.345426591608,-17.3522875107012,
21.0010643315316));
#170084=CARTESIAN_POINT('Ctrl Pts',(-17.4390035944696,-17.2766531277653,
20.9932277162184));
#170085=CARTESIAN_POINT('Ctrl Pts',(-17.4756950823505,-17.2489227520531,
20.9902669459361));
#170086=CARTESIAN_POINT('Ctrl Pts',(-17.5269190623262,-17.2127691336375,
20.9863123278379));
#170087=CARTESIAN_POINT('Ctrl Pts',(-17.5406895079049,-17.2032923334854,
20.9852661703942));
#170088=CARTESIAN_POINT('Ctrl Pts',(-17.5644677783493,-17.1873398606836,
20.9834904712766));
#170089=CARTESIAN_POINT('Ctrl Pts',(-17.574420510733,-17.18078390707,20.982756283555));
#170090=CARTESIAN_POINT('Ctrl Pts',(-17.5886445862378,-17.1715856699061,
20.9817204145142));
#170091=CARTESIAN_POINT('Ctrl Pts',(-17.59287057489,-17.1688741359681,20.9814143215289));
#170092=CARTESIAN_POINT('Ctrl Pts',(-17.6001692037068,-17.1642276684102,
20.9808885916387));
#170093=CARTESIAN_POINT('Ctrl Pts',(-17.6032372335233,-17.162285567204,
20.9806684816669));
#170094=CARTESIAN_POINT('Ctrl Pts',(-17.6091971208153,-17.1585343275622,
20.9802426318139));
#170095=CARTESIAN_POINT('Ctrl Pts',(-17.612088350825,-17.1567242866175,
20.9800368289607));
#170096=CARTESIAN_POINT('Ctrl Pts',(-17.6198980245481,-17.1518613110809,
20.9794829963599));
#170097=CARTESIAN_POINT('Ctrl Pts',(-17.6248246783332,-17.1488215233521,
20.9791358277436));
#170098=CARTESIAN_POINT('Ctrl Pts',(-17.6431404597721,-17.1376239978535,
20.9778531015));
#170099=CARTESIAN_POINT('Ctrl Pts',(-17.6566079933588,-17.1295946361591,
20.9769255817702));
#170100=CARTESIAN_POINT('Ctrl Pts',(-17.7862430427947,-17.0542454583023,
20.9681340851487));
#170101=CARTESIAN_POINT('Ctrl Pts',(-17.9084942705672,-16.997961680057,
20.9608714200922));
#170102=CARTESIAN_POINT('Ctrl Pts',(-18.1869591142976,-16.9005959526035,
20.9448516764622));
#170103=CARTESIAN_POINT('Ctrl Pts',(-18.3441739376419,-16.86500700228,20.9361044514156));
#170104=CARTESIAN_POINT('Ctrl Pts',(-18.5224430219259,-16.8455145698628,
20.9256316433863));
#170105=CARTESIAN_POINT('Ctrl Pts',(-18.5410187256382,-16.84373165439,20.9245345206191));
#170106=CARTESIAN_POINT('Ctrl Pts',(-18.5681154391477,-16.8414919897973,
20.9229246961221));
#170107=CARTESIAN_POINT('Ctrl Pts',(-18.5766198066782,-16.8408407875857,
20.9224180998174));
#170108=CARTESIAN_POINT('Ctrl Pts',(-18.5915593296888,-16.8397875992689,
20.9215257112069));
#170109=CARTESIAN_POINT('Ctrl Pts',(-18.5979928579074,-16.8393635839924,
20.9211406155685));
#170110=CARTESIAN_POINT('Ctrl Pts',(-18.610505430169,-16.8385963085087,
20.9203900514181));
#170111=CARTESIAN_POINT('Ctrl Pts',(-18.6165842213919,-16.838249871504,
20.9200246866073));
#170112=CARTESIAN_POINT('Ctrl Pts',(-18.6311460222534,-16.8374829872647,
20.9191476686883));
#170113=CARTESIAN_POINT('Ctrl Pts',(-18.6396301836557,-16.8370873605842,
20.9186352418486));
#170114=CARTESIAN_POINT('Ctrl Pts',(-18.6704146048268,-16.8358374525823,
20.9167705396065));
#170115=CARTESIAN_POINT('Ctrl Pts',(-18.6927250273156,-16.8352847743723,
20.9154088693828));
#170116=CARTESIAN_POINT('Ctrl Pts',(-18.8983629538489,-16.8334429315233,
20.9027594792591));
#170117=CARTESIAN_POINT('Ctrl Pts',(-19.0810906891775,-16.8556220084415,
20.8906948986998));
#170118=CARTESIAN_POINT('Ctrl Pts',(-19.337623703182,-16.9212426786108,
20.8732108564779));
#170119=CARTESIAN_POINT('Ctrl Pts',(-19.4153870026047,-16.9459964148468,
20.8678507079561));
#170120=CARTESIAN_POINT('Ctrl Pts',(-19.5255257817737,-16.9882023664138,
20.8603297433804));
#170121=CARTESIAN_POINT('Ctrl Pts',(-19.5591795516302,-17.0021042887357,
20.8580420997372));
#170122=CARTESIAN_POINT('Ctrl Pts',(-19.5993085431524,-17.0199062511952,
20.8553411458936));
#170123=CARTESIAN_POINT('Ctrl Pts',(-19.6061407962664,-17.0229806728898,
20.8548822451438));
#170124=CARTESIAN_POINT('Ctrl Pts',(-19.6167470999459,-17.0278212356537,
20.8541715103574));
#170125=CARTESIAN_POINT('Ctrl Pts',(-19.6205324220766,-17.0295623222269,
20.8539181837581));
#170126=CARTESIAN_POINT('Ctrl Pts',(-19.6275485583982,-17.0328145751237,
20.8534492878169));
#170127=CARTESIAN_POINT('Ctrl Pts',(-19.6307806650478,-17.0343227173574,
20.8532335425427));
#170128=CARTESIAN_POINT('Ctrl Pts',(-19.6380868132466,-17.0377543702729,
20.8527464286674));
#170129=CARTESIAN_POINT('Ctrl Pts',(-19.6421585242702,-17.0396827165784,
20.8524753631437));
#170130=CARTESIAN_POINT('Ctrl Pts',(-19.6544481791575,-17.0455511527693,
20.8516583326395));
#170131=CARTESIAN_POINT('Ctrl Pts',(-19.6626469890034,-17.0495313841809,
20.8511147944127));
#170132=CARTESIAN_POINT('Ctrl Pts',(-19.7255935316432,-17.0805935830074,
20.8469516357087));
#170133=CARTESIAN_POINT('Ctrl Pts',(-19.7791771967552,-17.1099832236455,
20.8434651876825));
#170134=CARTESIAN_POINT('Ctrl Pts',(-19.9708583098656,-17.2261788969541,
20.8309359318723));
#170135=CARTESIAN_POINT('Ctrl Pts',(-20.1000686775985,-17.3265342065346,
20.8223349060213));
#170136=CARTESIAN_POINT('Ctrl Pts',(-20.2731076958554,-17.4962774860746,
20.8088863626249));
#170137=CARTESIAN_POINT('Ctrl Pts',(-20.3265596629551,-17.5549558728225,
20.8043990523465));
#170138=CARTESIAN_POINT('Ctrl Pts',(-20.3888154825006,-17.6315265031988,
20.7986404092466));
#170139=CARTESIAN_POINT('Ctrl Pts',(-20.4008332352514,-17.6467293514953,
20.79750168058));
#170140=CARTESIAN_POINT('Ctrl Pts',(-20.4179160356804,-17.6689603452835,
20.7958421240072));
#170141=CARTESIAN_POINT('Ctrl Pts',(-20.4231495398368,-17.6758582369229,
20.7953279585968));
#170142=CARTESIAN_POINT('Ctrl Pts',(-20.4322170744103,-17.6879629844478,
20.7944269154874));
#170143=CARTESIAN_POINT('Ctrl Pts',(-20.436069863554,-17.6931556940374,
20.7940407786994));
#170144=CARTESIAN_POINT('Ctrl Pts',(-20.4434805340365,-17.7032398597072,
20.7932916276387));
#170145=CARTESIAN_POINT('Ctrl Pts',(-20.4470413638276,-17.7081290786947,
20.7929287332013));
#170146=CARTESIAN_POINT('Ctrl Pts',(-20.4554655364922,-17.7198007223967,
20.7920631596206));
#170147=CARTESIAN_POINT('Ctrl Pts',(-20.4603097930576,-17.7265967405258,
20.7915597506624));
#170148=CARTESIAN_POINT('Ctrl Pts',(-20.47743436792,-17.7509239195865,20.7897596960242));
#170149=CARTESIAN_POINT('Ctrl Pts',(-20.4894885235742,-17.7686120091074,
20.788454475028));
#170150=CARTESIAN_POINT('Ctrl Pts',(-20.5919346977185,-17.923950535541,
20.7770191365605));
#170151=CARTESIAN_POINT('Ctrl Pts',(-20.6661822790493,-18.0714329895054,
20.7662793853259));
#170152=CARTESIAN_POINT('Ctrl Pts',(-20.7225805788317,-18.2258896216873,
20.755413772291));
#170153=CARTESIAN_POINT('',(-20.8509997094765,-18.9531090880733,21.2890562789773));
#170154=CARTESIAN_POINT('Ctrl Pts',(-20.8509997094765,-18.9531090880733,
21.2890562789773));
#170155=CARTESIAN_POINT('Ctrl Pts',(-20.8509573539261,-19.0339563084801,
21.2842160173539));
#170156=CARTESIAN_POINT('Ctrl Pts',(-20.8462795783447,-19.1146414750005,
21.2793757557306));
#170157=CARTESIAN_POINT('Ctrl Pts',(-20.8370465901719,-19.1946603378517,
21.2745354941073));
#170158=CARTESIAN_POINT('Ctrl Pts',(-20.8277795525455,-19.2749742946103,
21.2696773825463));
#170159=CARTESIAN_POINT('Ctrl Pts',(-20.8139237784189,-19.354616746761,
21.2648192709853));
#170160=CARTESIAN_POINT('Ctrl Pts',(-20.7956102733323,-19.4330946693642,
21.2599611594243));
#170161=CARTESIAN_POINT('Ctrl Pts',(-20.7772067235592,-19.5119584558372,
21.2550791612762));
#170162=CARTESIAN_POINT('Ctrl Pts',(-20.754301638724,-19.5896459636135,
21.2501971631282));
#170163=CARTESIAN_POINT('Ctrl Pts',(-20.7270762122811,-19.6656779470036,
21.2453151649801));
#170164=CARTESIAN_POINT('Ctrl Pts',(-20.714146733797,-19.7017858807181,
21.2429966819199));
#170165=CARTESIAN_POINT('Ctrl Pts',(-20.700243557214,-19.7375207682869,
21.2406781988597));
#170166=CARTESIAN_POINT('Ctrl Pts',(-20.6853897271448,-19.7728331942566,
21.2383597157995));
#170167=CARTESIAN_POINT('Ctrl Pts',(-20.6572744235311,-19.8396724924615,
21.2339712951122));
#170168=CARTESIAN_POINT('Ctrl Pts',(-20.6256662222363,-19.9051959792736,
21.229582874425));
#170169=CARTESIAN_POINT('Ctrl Pts',(-20.5907099161381,-19.9690139071392,
21.2251944537377));
#170170=CARTESIAN_POINT('Ctrl Pts',(-20.5558054761045,-20.0327371458015,
21.2208125443251));
#170171=CARTESIAN_POINT('Ctrl Pts',(-20.5175630226924,-20.0947594296034,
21.2164306349125));
#170172=CARTESIAN_POINT('Ctrl Pts',(-20.4761752538898,-20.1547112640755,
21.2120487254999));
#170173=CARTESIAN_POINT('Ctrl Pts',(-20.434836104603,-20.214592671239,21.2076719636544));
#170174=CARTESIAN_POINT('Ctrl Pts',(-20.3903592525526,-20.2724080657538,
21.2032952018088));
#170175=CARTESIAN_POINT('Ctrl Pts',(-20.342982262568,-20.3278143329467,
21.1989184399633));
#170176=CARTESIAN_POINT('Ctrl Pts',(-20.295635309639,-20.3831854725149,
21.1945444529888));
#170177=CARTESIAN_POINT('Ctrl Pts',(-20.2453921796757,-20.4361501496307,
21.1901704660143));
#170178=CARTESIAN_POINT('Ctrl Pts',(-20.1925316651773,-20.4863970743179,
21.1857964790398));
#170179=CARTESIAN_POINT('Ctrl Pts',(-20.139687231237,-20.5366287135202,
21.1814238226644));
#170180=CARTESIAN_POINT('Ctrl Pts',(-20.0842273429024,-20.584143909571,
21.177051166289));
#170181=CARTESIAN_POINT('Ctrl Pts',(-20.0264675343393,-20.6286683251851,
21.1726785099136));
#170182=CARTESIAN_POINT('Ctrl Pts',(-19.9687062484273,-20.6731938796203,
21.1683057416968));
#170183=CARTESIAN_POINT('Ctrl Pts',(-19.9086453087151,-20.7147282088577,
21.16393297348));
#170184=CARTESIAN_POINT('Ctrl Pts',(-19.8466318572416,-20.7530384088772,
21.1595602052632));
#170185=CARTESIAN_POINT('Ctrl Pts',(-19.7845540695746,-20.7913883540227,
21.1551829004941));
#170186=CARTESIAN_POINT('Ctrl Pts',(-19.7205201370247,-20.8265072376108,
21.1508055957251));
#170187=CARTESIAN_POINT('Ctrl Pts',(-19.654903893158,-20.8582069718597,
21.146428290956));
#170188=CARTESIAN_POINT('Ctrl Pts',(-19.589251822749,-20.8899240141987,
21.1420485961737));
#170189=CARTESIAN_POINT('Ctrl Pts',(-19.5220161657843,-20.9182180030709,
21.1376689013914));
#170190=CARTESIAN_POINT('Ctrl Pts',(-19.4535904234765,-20.9429491762576,
21.133289206609));
#170191=CARTESIAN_POINT('Ctrl Pts',(-19.3850434522868,-20.9677241653004,
21.1289017523858));
#170192=CARTESIAN_POINT('Ctrl Pts',(-19.3153026471293,-20.9889235930605,
21.1245142981626));
#170193=CARTESIAN_POINT('Ctrl Pts',(-19.2447757667322,-21.0064578642842,
21.1201268439394));
#170194=CARTESIAN_POINT('Ctrl Pts',(-19.1968575236042,-21.018371215149,
21.1171458656656));
#170195=CARTESIAN_POINT('Ctrl Pts',(-19.1485766551865,-21.028593691043,
21.1141648873919));
#170196=CARTESIAN_POINT('Ctrl Pts',(-19.1000625450044,-21.0371108395347,
21.1111839091181));
#170197=CARTESIAN_POINT('Ctrl Pts',(-19.0286448032708,-21.0496489549201,
21.1067956036196));
#170198=CARTESIAN_POINT('Ctrl Pts',(-18.9564428174331,-21.0585380613871,
21.102407298121));
#170199=CARTESIAN_POINT('Ctrl Pts',(-18.8838626580299,-21.0636889410442,
21.0980189926225));
#170200=CARTESIAN_POINT('Ctrl Pts',(-18.8113901771551,-21.0688321789552,
21.0936371975296));
#170201=CARTESIAN_POINT('Ctrl Pts',(-18.7385411136489,-21.0702481657021,
21.0892554024367));
#170202=CARTESIAN_POINT('Ctrl Pts',(-18.6657304393715,-21.0678989264829,
21.0848736073437));
#170203=CARTESIAN_POINT('Ctrl Pts',(-18.5930052691539,-21.0655524460555,
21.0804969579424));
#170204=CARTESIAN_POINT('Ctrl Pts',(-18.5203188783214,-21.059449538749,
21.076120308541));
#170205=CARTESIAN_POINT('Ctrl Pts',(-18.448088343777,-21.049604234558,21.0717436591396));
#170206=CARTESIAN_POINT('Ctrl Pts',(-18.3759035845749,-21.0397651697252,
21.0673697833938));
#170207=CARTESIAN_POINT('Ctrl Pts',(-18.3041745852159,-21.0261884787699,
21.062995907648));
#170208=CARTESIAN_POINT('Ctrl Pts',(-18.2333139789055,-21.0089400837848,
21.0586220319021));
#170209=CARTESIAN_POINT('Ctrl Pts',(-18.1624749070484,-20.9916969305662,
21.0542494853719));
#170210=CARTESIAN_POINT('Ctrl Pts',(-18.0925041726962,-20.9707844025933,
21.0498769388417));
#170211=CARTESIAN_POINT('Ctrl Pts',(-18.0238032249561,-20.9463193176413,
21.0455043923115));
#170212=CARTESIAN_POINT('Ctrl Pts',(-17.9551004955794,-20.9218535982309,
21.041131732387));
#170213=CARTESIAN_POINT('Ctrl Pts',(-17.8876680719231,-20.8938353026274,
21.0367590724626));
#170214=CARTESIAN_POINT('Ctrl Pts',(-17.8218896723665,-20.8624302526458,
21.0323864125382));
#170215=CARTESIAN_POINT('Ctrl Pts',(-17.7560429813199,-20.8309925977715,
21.0280092128946));
#170216=CARTESIAN_POINT('Ctrl Pts',(-17.6918541791272,-20.7961613765664,
21.023632013251));
#170217=CARTESIAN_POINT('Ctrl Pts',(-17.6296837477988,-20.7581491120958,
21.0192548136074));
#170218=CARTESIAN_POINT('Ctrl Pts',(-17.5674793476667,-20.7201160784086,
21.0148752223408));
#170219=CARTESIAN_POINT('Ctrl Pts',(-17.5072959123103,-20.6788988137273,
21.0104956310741));
#170220=CARTESIAN_POINT('Ctrl Pts',(-17.4494639340252,-20.634752535345,
21.0061160398075));
#170221=CARTESIAN_POINT('Ctrl Pts',(-17.3915294434579,-20.5905280037906,
21.0017286853291));
#170222=CARTESIAN_POINT('Ctrl Pts',(-17.3359551017082,-20.5433644028354,
20.9973413308507));
#170223=CARTESIAN_POINT('Ctrl Pts',(-17.2830369348489,-20.4935560916059,
20.9929539763722));
#170224=CARTESIAN_POINT('Ctrl Pts',(-17.2470699869645,-20.4597028226716,
20.9899720183937));
#170225=CARTESIAN_POINT('Ctrl Pts',(-17.2123293058517,-20.4246286086914,
20.9869900604152));
#170226=CARTESIAN_POINT('Ctrl Pts',(-17.1788971544343,-20.3884345232949,
20.9840081024366));
#170227=CARTESIAN_POINT('Ctrl Pts',(-17.1297001013421,-20.3351731486785,
20.979620004789));
#170228=CARTESIAN_POINT('Ctrl Pts',(-17.0831463900084,-20.2792773756617,
20.9752319071414));
#170229=CARTESIAN_POINT('Ctrl Pts',(-17.0395308416818,-20.2210402954628,
20.9708438094938));
#170230=CARTESIAN_POINT('Ctrl Pts',(-16.9959800453897,-20.1628896745558,
20.9664622264554));
#170231=CARTESIAN_POINT('Ctrl Pts',(-16.9553590396968,-20.1024050295693,
20.9620806434169));
#170232=CARTESIAN_POINT('Ctrl Pts',(-16.9179243810532,-20.0399146778434,
20.9576990603784));
#170233=CARTESIAN_POINT('Ctrl Pts',(-16.8805337302903,-19.9774977892675,
20.9533226282934));
#170234=CARTESIAN_POINT('Ctrl Pts',(-16.8463222321173,-19.9130802896936,
20.9489461962084));
#170235=CARTESIAN_POINT('Ctrl Pts',(-16.8155038577208,-19.8470204199123,
20.9445697641234));
#170236=CARTESIAN_POINT('Ctrl Pts',(-16.7847050371391,-19.781002464167,
20.9401961088215));
#170237=CARTESIAN_POINT('Ctrl Pts',(-16.7572952721812,-19.7133446418889,
20.9358224535196));
#170238=CARTESIAN_POINT('Ctrl Pts',(-16.7334424981437,-19.6444295500383,
20.9314487982177));
#170239=CARTESIAN_POINT('Ctrl Pts',(-16.7095969886214,-19.5755354467209,
20.9270764749406));
#170240=CARTESIAN_POINT('Ctrl Pts',(-16.6893064770216,-19.5053852896205,
20.9227041516635));
#170241=CARTESIAN_POINT('Ctrl Pts',(-16.6726900512339,-19.4343798245343,
20.9183318283864));
#170242=CARTESIAN_POINT('Ctrl Pts',(-16.6560732039841,-19.3633725584528,
20.9139593942089));
#170243=CARTESIAN_POINT('Ctrl Pts',(-16.6431307355402,-19.2915104114853,
20.9095869600314));
#170244=CARTESIAN_POINT('Ctrl Pts',(-16.6339309326538,-19.2192057491441,
20.9052145258539));
#170245=CARTESIAN_POINT('Ctrl Pts',(-16.6247215828182,-19.1468260537894,
20.9008375542524));
#170246=CARTESIAN_POINT('Ctrl Pts',(-16.6192627140126,-19.0740034057825,
20.8964605826508));
#170247=CARTESIAN_POINT('Ctrl Pts',(-16.6175707675104,-19.0011559138216,
20.8920836110493));
#170248=CARTESIAN_POINT('Ctrl Pts',(-16.6158778971444,-18.9282686444977,
20.8877042494631));
#170249=CARTESIAN_POINT('Ctrl Pts',(-16.6179560305416,-18.8553569867552,
20.8833248878769));
#170250=CARTESIAN_POINT('Ctrl Pts',(-16.6237694768944,-18.782836944478,
20.8789455262907));
#170251=CARTESIAN_POINT('Ctrl Pts',(-16.6295932284966,-18.7101883490033,
20.8745584015963));
#170252=CARTESIAN_POINT('Ctrl Pts',(-16.6391654523683,-18.6379332339321,
20.8701712769019));
#170253=CARTESIAN_POINT('Ctrl Pts',(-16.6523988893426,-18.5664798110215,
20.8657841522075));
#170254=CARTESIAN_POINT('Ctrl Pts',(-16.6613997601799,-18.5178799626416,
20.8628002000567));
#170255=CARTESIAN_POINT('Ctrl Pts',(-16.6720933057598,-18.4696507787821,
20.859816247906));
#170256=CARTESIAN_POINT('Ctrl Pts',(-16.6844389804171,-18.4219163962107,
20.8568322957552));
#170257=CARTESIAN_POINT('Ctrl Pts',(-16.7025947174696,-18.3517174866827,
20.8524440503065));
#170258=CARTESIAN_POINT('Ctrl Pts',(-16.7243966047991,-18.2823154178057,
20.8480558048578));
#170259=CARTESIAN_POINT('Ctrl Pts',(-16.7497577485801,-18.2141167519993,
20.8436675594091));
#170260=CARTESIAN_POINT('Ctrl Pts',(-16.7750812545399,-18.1460192980786,
20.8392858264426));
#170261=CARTESIAN_POINT('Ctrl Pts',(-16.8039533643146,-18.0791221502751,
20.834904093476));
#170262=CARTESIAN_POINT('Ctrl Pts',(-16.8362368533681,-18.0138187598946,
20.8305223605095));
#170263=CARTESIAN_POINT('Ctrl Pts',(-16.8684824095669,-17.9485921005021,
20.826145776046));
#170264=CARTESIAN_POINT('Ctrl Pts',(-16.9041311697296,-17.8849559087621,
20.8217691915824));
#170265=CARTESIAN_POINT('Ctrl Pts',(-16.9429976989673,-17.8232840225745,
20.8173926071189));
#170266=CARTESIAN_POINT('Ctrl Pts',(-16.9818395815048,-17.7616512448053,
20.813018798009));
#170267=CARTESIAN_POINT('Ctrl Pts',(-17.0238949279354,-17.7019807081629,
20.8086449888991));
#170268=CARTESIAN_POINT('Ctrl Pts',(-17.0689329066922,-17.6446207226732,
20.8042711797893));
#170269=CARTESIAN_POINT('Ctrl Pts',(-17.1139571817387,-17.587278190112,
20.7998987014987));
#170270=CARTESIAN_POINT('Ctrl Pts',(-17.1619619896782,-17.5322451921335,
20.7955262232082));
#170271=CARTESIAN_POINT('Ctrl Pts',(-17.2126747998581,-17.4798387875598,
20.7911537449176));
#170272=CARTESIAN_POINT('Ctrl Pts',(-17.2633889076796,-17.4274310420089,
20.7867811547439));
#170273=CARTESIAN_POINT('Ctrl Pts',(-17.3168108184396,-17.3776503685512,
20.7824085645702));
#170274=CARTESIAN_POINT('Ctrl Pts',(-17.3726307347287,-17.3307773985123,
20.7780359743965));
#170275=CARTESIAN_POINT('Ctrl Pts',(-17.428508580755,-17.2838557838494,
20.7736588463622));
#170276=CARTESIAN_POINT('Ctrl Pts',(-17.4867890308601,-17.2398482083165,
20.7692817183279));
#170277=CARTESIAN_POINT('Ctrl Pts',(-17.547129396645,-17.1989948172091,
20.7649045902936));
#170278=CARTESIAN_POINT('Ctrl Pts',(-17.6075027159868,-17.1581191149253,
20.7605250717876));
#170279=CARTESIAN_POINT('Ctrl Pts',(-17.6699377776663,-17.1204012763226,
20.7561455532815));
#170280=CARTESIAN_POINT('Ctrl Pts',(-17.7340654457233,-17.0860364721776,
20.7517660347755));
#170281=CARTESIAN_POINT('Ctrl Pts',(-17.7983067720839,-17.0516107606978,
20.7473787541185));
#170282=CARTESIAN_POINT('Ctrl Pts',(-17.864246258806,-17.0205501570155,
20.7429914734614));
#170283=CARTESIAN_POINT('Ctrl Pts',(-17.9314934095092,-16.9930022531359,
20.7386041928044));
#170284=CARTESIAN_POINT('Ctrl Pts',(-17.9772094713291,-16.9742745945867,
20.7356216248942));
#170285=CARTESIAN_POINT('Ctrl Pts',(-18.0235294787558,-16.9571693380886,
20.732639056984));
#170286=CARTESIAN_POINT('Ctrl Pts',(-18.0703272882045,-16.9417195390648,
20.7296564890738));
#170287=CARTESIAN_POINT('Ctrl Pts',(-18.139180375299,-16.9189884247175,
20.7252682706827));
#170288=CARTESIAN_POINT('Ctrl Pts',(-18.2093370331468,-16.8997544122152,
20.7208800522916));
#170289=CARTESIAN_POINT('Ctrl Pts',(-18.2804083783847,-16.884164503448,
20.7164918339006));
#170290=CARTESIAN_POINT('Ctrl Pts',(-18.3513742467947,-16.8685977316303,
20.7121101280548));
#170291=CARTESIAN_POINT('Ctrl Pts',(-18.4232516405218,-16.8566644300181,
20.707728422209));
#170292=CARTESIAN_POINT('Ctrl Pts',(-18.4956354571152,-16.8484621836783,
20.7033467163632));
#170293=CARTESIAN_POINT('Ctrl Pts',(-18.5679342234102,-16.8402695749002,
20.6989701589803));
#170294=CARTESIAN_POINT('Ctrl Pts',(-18.6407377535873,-16.8357993666837,
20.6945936015973));
#170295=CARTESIAN_POINT('Ctrl Pts',(-18.7136313412727,-16.8350979905197,
20.6902170442144));
#170296=CARTESIAN_POINT('Ctrl Pts',(-18.7864787048096,-16.8343970591207,
20.685843262146));
#170297=CARTESIAN_POINT('Ctrl Pts',(-18.8594155313779,-16.837460222459,
20.6814694800777));
#170298=CARTESIAN_POINT('Ctrl Pts',(-18.932024006899,-16.8442819228626,
20.6770956980093));
#170299=CARTESIAN_POINT('Ctrl Pts',(-19.0046103910108,-16.8511015477375,
20.6727232466811));
#170300=CARTESIAN_POINT('Ctrl Pts',(-19.0768681424401,-16.8616773942849,
20.6683507953528));
#170301=CARTESIAN_POINT('Ctrl Pts',(-19.1483831533474,-16.8759519268037,
20.6639783440246));
#170302=CARTESIAN_POINT('Ctrl Pts',(-19.2198999961485,-16.890226824972,
20.6596057806937));
#170303=CARTESIAN_POINT('Ctrl Pts',(-19.2906735880014,-16.9082005008351,
20.6552332173629));
#170304=CARTESIAN_POINT('Ctrl Pts',(-19.3603002789774,-16.9297643657197,
20.6508606540321));
#170305=CARTESIAN_POINT('Ctrl Pts',(-19.4299992346993,-16.951350611493,
20.6464835524678));
#170306=CARTESIAN_POINT('Ctrl Pts',(-19.4985484511517,-16.976534342916,
20.6421064509035));
#170307=CARTESIAN_POINT('Ctrl Pts',(-19.5655605174569,-17.005157400865,
20.6377293493392));
#170308=CARTESIAN_POINT('Ctrl Pts',(-19.6326091837084,-17.033796091855,
20.6333498571355));
#170309=CARTESIAN_POINT('Ctrl Pts',(-19.6981185947722,-17.0658776370537,
20.6289703649319));
#170310=CARTESIAN_POINT('Ctrl Pts',(-19.7617248407813,-17.1011972953226,
20.6245908727283));
#170311=CARTESIAN_POINT('Ctrl Pts',(-19.8254438298318,-17.1365795582247,
20.6202036178079));
#170312=CARTESIAN_POINT('Ctrl Pts',(-19.8872525078967,-17.1752111400653,
20.6158163628875));
#170313=CARTESIAN_POINT('Ctrl Pts',(-19.9468154094471,-17.2168435855498,
20.6114291079671));
#170314=CARTESIAN_POINT('Ctrl Pts',(-19.9873110573495,-17.2451486682401,
20.6084462994422));
#170315=CARTESIAN_POINT('Ctrl Pts',(-20.0267692624342,-17.2748399740111,
20.6054634909173));
#170316=CARTESIAN_POINT('Ctrl Pts',(-20.0650939280144,-17.3058293056906,
20.6024806823923));
#170317=CARTESIAN_POINT('Ctrl Pts',(-20.1207334278707,-17.3508194155695,
20.5981502604048));
#170318=CARTESIAN_POINT('Ctrl Pts',(-20.174211694955,-17.3987327328762,
20.5938198384172));
#170319=CARTESIAN_POINT('Ctrl Pts',(-20.2251992647985,-17.4493311234127,
20.5894894164297));
#170320=CARTESIAN_POINT('Ctrl Pts',(-20.2761150683178,-17.4998582954048,
20.5851650896231));
#170321=CARTESIAN_POINT('Ctrl Pts',(-20.3245467768446,-17.5530627009004,
20.5808407628166));
#170322=CARTESIAN_POINT('Ctrl Pts',(-20.3701971545491,-17.6086653911086,
20.5765164360101));
#170323=CARTESIAN_POINT('Ctrl Pts',(-20.4157961614946,-17.6642055111358,
20.5721969754054));
#170324=CARTESIAN_POINT('Ctrl Pts',(-20.4586197368312,-17.7221381775607,
20.5678775148007));
#170325=CARTESIAN_POINT('Ctrl Pts',(-20.498408150765,-17.782148352348,20.5635580541959));
#170326=CARTESIAN_POINT('Ctrl Pts',(-20.5381709755269,-17.8421199327174,
20.5592413715713));
#170327=CARTESIAN_POINT('Ctrl Pts',(-20.574902238587,-17.9041659577839,
20.5549246889466));
#170328=CARTESIAN_POINT('Ctrl Pts',(-20.6083841459909,-17.967940513354,
20.5506080063219));
#170329=CARTESIAN_POINT('Ctrl Pts',(-20.6418605335062,-18.0317045549341,
20.5462920353534));
#170330=CARTESIAN_POINT('Ctrl Pts',(-20.6720883940015,-18.0971961244752,
20.5419760643849));
#170331=CARTESIAN_POINT('Ctrl Pts',(-20.6988955789411,-18.1640441866084,
20.5376600934164));
#170332=CARTESIAN_POINT('Ctrl Pts',(-20.7071130186217,-18.184535704818,
20.5363370812771));
#170333=CARTESIAN_POINT('Ctrl Pts',(-20.7150093677705,-18.2051545331966,
20.5350140691378));
#170334=CARTESIAN_POINT('Ctrl Pts',(-20.7225805737622,-18.2258896078036,
20.5336910569984));
#170335=CARTESIAN_POINT('Ctrl Pts',(-20.7225805737622,-18.2258896078036,
21.3335535462005));
#170336=CARTESIAN_POINT('Ctrl Pts',(-20.7478889850652,-18.2952011279398,
21.3291191954399));
#170337=CARTESIAN_POINT('Ctrl Pts',(-20.7695971613257,-18.3659128814929,
21.3246848446794));
#170338=CARTESIAN_POINT('Ctrl Pts',(-20.7875590779851,-18.4376225965061,
21.3202504939188));
#170339=CARTESIAN_POINT('Ctrl Pts',(-20.8055066098553,-18.5092748828416,
21.3158196944051));
#170340=CARTESIAN_POINT('Ctrl Pts',(-20.8197137296134,-18.5819230936247,
21.3113888948915));
#170341=CARTESIAN_POINT('Ctrl Pts',(-20.830084178873,-18.6551496756305,
21.3069580953778));
#170342=CARTESIAN_POINT('Ctrl Pts',(-20.8404495304526,-18.728340262505,
21.3025294738602));
#170343=CARTESIAN_POINT('Ctrl Pts',(-20.8469818942704,-18.8021081961854,
21.2981008523426));
#170344=CARTESIAN_POINT('Ctrl Pts',(-20.8496363359742,-18.8760270185819,
21.2936722308251));
#170345=CARTESIAN_POINT('Ctrl Pts',(-20.8505585774226,-18.9017088791887,
21.2921335802242));
#170346=CARTESIAN_POINT('Ctrl Pts',(-20.8510131736972,-18.9274089012658,
21.2905949296234));
#170347=CARTESIAN_POINT('Ctrl Pts',(-20.8509997094769,-18.9531090873175,
21.2890562790225));
#170348=CARTESIAN_POINT('Origin',(18.734,-18.952,0.));
#170349=CARTESIAN_POINT('',(16.7454193692319,-18.2258897639242,0.755484063719886));
#170350=CARTESIAN_POINT('',(16.7454193692601,-18.2258897638472,0.534177402183209));
#170351=CARTESIAN_POINT('',(16.7454193692319,-18.2258897639242,0.));
#170352=CARTESIAN_POINT('',(16.6170002905275,-18.9508909042358,0.710943721022754));
#170353=CARTESIAN_POINT('Ctrl Pts',(16.6170002905275,-18.9508909042358,
0.710943721022754));
#170354=CARTESIAN_POINT('Ctrl Pts',(16.6170426220087,-18.8700901868306,
0.715781198687434));
#170355=CARTESIAN_POINT('Ctrl Pts',(16.6217150376884,-18.7894513354829,
0.720618676352114));
#170356=CARTESIAN_POINT('Ctrl Pts',(16.6309374829181,-18.7094777345376,
0.725456154016795));
#170357=CARTESIAN_POINT('Ctrl Pts',(16.6404786381714,-18.6267403992884,
0.730460805633977));
#170358=CARTESIAN_POINT('Ctrl Pts',(16.6548898613221,-18.5447154887152,
0.735465457251158));
#170359=CARTESIAN_POINT('Ctrl Pts',(16.6740271623484,-18.4639416959648,
0.74047010886834));
#170360=CARTESIAN_POINT('Ctrl Pts',(16.6931644633748,-18.3831679032145,
0.745474760485522));
#170361=CARTESIAN_POINT('Ctrl Pts',(16.7170276379269,-18.303645515244,0.750479412102703));
#170362=CARTESIAN_POINT('Ctrl Pts',(16.7454193692319,-18.2258897639242,
0.755484063719885));
#170363=CARTESIAN_POINT('',(17.1140597194292,-17.5891051077268,2.19245913216589E-7));
#170364=CARTESIAN_POINT('Ctrl Pts',(17.1140597194292,-17.5891051077268,
2.19245913216589E-7));
#170365=CARTESIAN_POINT('Ctrl Pts',(17.1607064768662,-17.5336606550705,
0.00438522828538332));
#170366=CARTESIAN_POINT('Ctrl Pts',(17.2102946586576,-17.480504861525,0.00877023732485342));
#170367=CARTESIAN_POINT('Ctrl Pts',(17.2625708870035,-17.4299667002899,
0.0131552463643235));
#170368=CARTESIAN_POINT('Ctrl Pts',(17.3147694940965,-17.3795035795756,
0.0175337444157921));
#170369=CARTESIAN_POINT('Ctrl Pts',(17.3696478802627,-17.3316507087742,
0.0219122424672607));
#170370=CARTESIAN_POINT('Ctrl Pts',(17.4269129074637,-17.2867035301409,
0.0262907405187293));
#170371=CARTESIAN_POINT('Ctrl Pts',(17.4841105391582,-17.2418092500745,
0.0306640854932059));
#170372=CARTESIAN_POINT('Ctrl Pts',(17.5436888539646,-17.1998141657851,
0.0350374304676826));
#170373=CARTESIAN_POINT('Ctrl Pts',(17.6053196809547,-17.1609752270279,
0.0394107754421593));
#170374=CARTESIAN_POINT('Ctrl Pts',(17.6669115101639,-17.1221608641606,
0.0437813531205117));
#170375=CARTESIAN_POINT('Ctrl Pts',(17.7305528669284,-17.0864989413484,
0.0481519307988641));
#170376=CARTESIAN_POINT('Ctrl Pts',(17.7958856448177,-17.0542037894966,
0.0525225084772165));
#170377=CARTESIAN_POINT('Ctrl Pts',(17.8611987192176,-17.0219183774295,
0.0568917680479646));
#170378=CARTESIAN_POINT('Ctrl Pts',(17.9282017691103,-16.9929979344005,
0.0612610276187128));
#170379=CARTESIAN_POINT('Ctrl Pts',(17.9965125678453,-16.9676106008614,
0.065630287189461));
#170380=CARTESIAN_POINT('Ctrl Pts',(18.0648253874043,-16.9422225162941,
0.0699996760151008));
#170381=CARTESIAN_POINT('Ctrl Pts',(18.1344455789652,-16.9203679149719,
0.0743690648407405));
#170382=CARTESIAN_POINT('Ctrl Pts',(18.20497303869,-16.9021659886208,0.0787384536663803));
#170383=CARTESIAN_POINT('Ctrl Pts',(18.2755722935749,-16.8839455331716,
0.0831122904187001));
#170384=CARTESIAN_POINT('Ctrl Pts',(18.3470801915498,-16.8693852963437,
0.0874861271710198));
#170385=CARTESIAN_POINT('Ctrl Pts',(18.4190844938148,-16.8585537446679,
0.0918599639233396));
#170386=CARTESIAN_POINT('Ctrl Pts',(18.4911286186645,-16.8477162025113,
0.0962362196628415));
#170387=CARTESIAN_POINT('Ctrl Pts',(18.563669213288,-16.8406114978773,0.100612475402343));
#170388=CARTESIAN_POINT('Ctrl Pts',(18.6362896320945,-16.8372561185799,
0.104988731141845));
#170389=CARTESIAN_POINT('Ctrl Pts',(18.7090341909997,-16.8338950034698,
0.109372467818922));
#170390=CARTESIAN_POINT('Ctrl Pts',(18.7818583632858,-16.8342960068782,
0.113756204495998));
#170391=CARTESIAN_POINT('Ctrl Pts',(18.8543469087348,-16.8384234999513,
0.118139941173075));
#170392=CARTESIAN_POINT('Ctrl Pts',(18.8963550317498,-16.8408154397493,
0.120680377713149));
#170393=CARTESIAN_POINT('Ctrl Pts',(18.9382505435929,-16.8444579003275,
0.123220814253224));
#170394=CARTESIAN_POINT('Ctrl Pts',(18.9799541383555,-16.8493360796775,
0.125761250793299));
#170395=CARTESIAN_POINT('Ctrl Pts',(19.0521147745614,-16.8577768994061,
0.130157023340392));
#170396=CARTESIAN_POINT('Ctrl Pts',(19.1239757332627,-16.8699525193612,
0.134552795887486));
#170397=CARTESIAN_POINT('Ctrl Pts',(19.1951211678868,-16.8858305324764,
0.13894856843458));
#170398=CARTESIAN_POINT('Ctrl Pts',(19.2661637754886,-16.901685596982,0.143337987739133));
#170399=CARTESIAN_POINT('Ctrl Pts',(19.3364924469683,-16.9212323267425,
0.147727407043687));
#170400=CARTESIAN_POINT('Ctrl Pts',(19.4056976986062,-16.9443866901997,
0.152116826348241));
#170401=CARTESIAN_POINT('Ctrl Pts',(19.4748249321718,-16.9675149507419,
0.156501297270635));
#170402=CARTESIAN_POINT('Ctrl Pts',(19.5428308084352,-16.9942426135354,
0.160885768193029));
#170403=CARTESIAN_POINT('Ctrl Pts',(19.6093188916083,-17.0244352571201,
0.165270239115423));
#170404=CARTESIAN_POINT('Ctrl Pts',(19.6757666906327,-17.0546096074275,
0.169652053551575));
#170405=CARTESIAN_POINT('Ctrl Pts',(19.7406980849853,-17.088244574323,0.174033867987726));
#170406=CARTESIAN_POINT('Ctrl Pts',(19.8037359157051,-17.125157349236,0.178415682423878));
#170407=CARTESIAN_POINT('Ctrl Pts',(19.8667561395948,-17.1620598141978,
0.182796272993961));
#170408=CARTESIAN_POINT('Ctrl Pts',(19.9278834356516,-17.2022380266861,
0.187176863564045));
#170409=CARTESIAN_POINT('Ctrl Pts',(19.9867660616864,-17.24546368492,0.191557454134129));
#170410=CARTESIAN_POINT('Ctrl Pts',(20.0456514706291,-17.2886913860829,
0.195938251739475));
#170411=CARTESIAN_POINT('Ctrl Pts',(20.1022916128046,-17.3349665330801,
0.200319049344822));
#170412=CARTESIAN_POINT('Ctrl Pts',(20.1563658617049,-17.3840190194213,
0.204699846950169));
#170413=CARTESIAN_POINT('Ctrl Pts',(20.2104972294522,-17.4331233201015,
0.209085272009677));
#170414=CARTESIAN_POINT('Ctrl Pts',(20.2620569360997,-17.4850104938254,
0.213470697069185));
#170415=CARTESIAN_POINT('Ctrl Pts',(20.31076005625,-17.5393724039881,0.217856122128693));
#170416=CARTESIAN_POINT('Ctrl Pts',(20.3594904212649,-17.5937647245818,
0.222244000425515));
#170417=CARTESIAN_POINT('Ctrl Pts',(20.4053607162011,-17.6506341638861,
0.226631878722337));
#170418=CARTESIAN_POINT('Ctrl Pts',(20.448127016551,-17.7096403213521,0.231019757019159));
#170419=CARTESIAN_POINT('Ctrl Pts',(20.490969053225,-17.7687509748683,0.23541540596179));
#170420=CARTESIAN_POINT('Ctrl Pts',(20.530695856384,-17.8300054996601,0.239811054904422));
#170421=CARTESIAN_POINT('Ctrl Pts',(20.5671077585182,-17.8930359091734,
0.244206703847054));
#170422=CARTESIAN_POINT('Ctrl Pts',(20.5912140801738,-17.9347648834029,
0.247116821722947));
#170423=CARTESIAN_POINT('Ctrl Pts',(20.6138684164928,-17.9772717133338,
0.25002693959884));
#170424=CARTESIAN_POINT('Ctrl Pts',(20.6350244530402,-18.0204448331188,
0.252937057474733));
#170425=CARTESIAN_POINT('Ctrl Pts',(20.6668851000169,-18.0854628493841,
0.257319647668148));
#170426=CARTESIAN_POINT('Ctrl Pts',(20.6954700316101,-18.1522473407963,
0.261702237861564));
#170427=CARTESIAN_POINT('Ctrl Pts',(20.7205801862023,-18.2204344432736,
0.266084828054979));
#170428=CARTESIAN_POINT('Ctrl Pts',(20.7456525615807,-18.2885189555772,
0.270460824469325));
#170429=CARTESIAN_POINT('Ctrl Pts',(20.767260371406,-18.3580014400402,0.274836820883671));
#170430=CARTESIAN_POINT('Ctrl Pts',(20.7852512326706,-18.428495099863,0.279212817298018));
#170431=CARTESIAN_POINT('Ctrl Pts',(20.8032205403916,-18.4989043063546,
0.283583571149047));
#170432=CARTESIAN_POINT('Ctrl Pts',(20.8175813879169,-18.5703218155193,
0.287954325000076));
#170433=CARTESIAN_POINT('Ctrl Pts',(20.8282307190733,-18.6423442309759,
0.292325078851105));
#170434=CARTESIAN_POINT('Ctrl Pts',(20.8388731539879,-18.7143200065093,
0.296693002310748));
#170435=CARTESIAN_POINT('Ctrl Pts',(20.845808770299,-18.7868994338195,0.301060925770392));
#170436=CARTESIAN_POINT('Ctrl Pts',(20.8489855691776,-18.8596688450712,
0.305428849230036));
#170437=CARTESIAN_POINT('Ctrl Pts',(20.8521613662237,-18.9324153078248,
0.309795395225144));
#170438=CARTESIAN_POINT('Ctrl Pts',(20.8515806778355,-19.0053511525544,
0.314161941220252));
#170439=CARTESIAN_POINT('Ctrl Pts',(20.8472434965741,-19.0780592090538,
0.31852848721536));
#170440=CARTESIAN_POINT('Ctrl Pts',(20.8429062422304,-19.1507684906964,
0.322895106787516));
#170441=CARTESIAN_POINT('Ctrl Pts',(20.8348124001615,-19.2232494936619,
0.327261726359673));
#170442=CARTESIAN_POINT('Ctrl Pts',(20.8230139692876,-19.2950883794611,
0.331628345931829));
#170443=CARTESIAN_POINT('Ctrl Pts',(20.8112033262544,-19.3670016232775,
0.335999485245201));
#170444=CARTESIAN_POINT('Ctrl Pts',(20.7956805170945,-19.4382709444889,
0.340370624558573));
#170445=CARTESIAN_POINT('Ctrl Pts',(20.7765488721863,-19.5084917831654,
0.344741763871945));
#170446=CARTESIAN_POINT('Ctrl Pts',(20.757406850392,-19.5787507091908,0.349115274064266));
#170447=CARTESIAN_POINT('Ctrl Pts',(20.7346522472,-19.6479595605984,0.353488784256587));
#170448=CARTESIAN_POINT('Ctrl Pts',(20.7084377550415,-19.7157306799303,
0.357862294448908));
#170449=CARTESIAN_POINT('Ctrl Pts',(20.682176526986,-19.7836226234244,0.362243601852049));
#170450=CARTESIAN_POINT('Ctrl Pts',(20.6524432899172,-19.8500712742597,
0.366624909255189));
#170451=CARTESIAN_POINT('Ctrl Pts',(20.6194379320409,-19.914711173936,0.37100621665833));
#170452=CARTESIAN_POINT('Ctrl Pts',(20.5965704686666,-19.9594963431776,
0.374041765824275));
#170453=CARTESIAN_POINT('Ctrl Pts',(20.5721332694026,-20.0034137682888,
0.377077314990221));
#170454=CARTESIAN_POINT('Ctrl Pts',(20.5462048528608,-20.0463502964169,
0.380112864156167));
#170455=CARTESIAN_POINT('Ctrl Pts',(20.5087129331597,-20.1084355711665,
0.384502201445418));
#170456=CARTESIAN_POINT('Ctrl Pts',(20.4679538690257,-20.1687127167994,
0.388891538734668));
#170457=CARTESIAN_POINT('Ctrl Pts',(20.424127447363,-20.2268169326104,0.393280876023919));
#170458=CARTESIAN_POINT('Ctrl Pts',(20.3803660122869,-20.2848349904712,
0.397663704726859));
#170459=CARTESIAN_POINT('Ctrl Pts',(20.333546536813,-20.3406861331264,0.4020465334298));
#170460=CARTESIAN_POINT('Ctrl Pts',(20.2839132740569,-20.3940325387807,
0.40642936213274));
#170461=CARTESIAN_POINT('Ctrl Pts',(20.234338311065,-20.4473162831732,0.410807042717946));
#170462=CARTESIAN_POINT('Ctrl Pts',(20.181956453283,-20.4981007839427,0.415184723303152));
#170463=CARTESIAN_POINT('Ctrl Pts',(20.1270525278191,-20.5460808181321,
0.419562403888358));
#170464=CARTESIAN_POINT('Ctrl Pts',(20.0721834146416,-20.5940304301855,
0.42393730876912));
#170465=CARTESIAN_POINT('Ctrl Pts',(20.0147957688626,-20.6391787874444,
0.428312213649883));
#170466=CARTESIAN_POINT('Ctrl Pts',(19.9552106047207,-20.6812581238548,
0.432687118530645));
#170467=CARTESIAN_POINT('Ctrl Pts',(19.8956435930083,-20.72332464093,0.437060690610634));
#170468=CARTESIAN_POINT('Ctrl Pts',(19.8338807856146,-20.7623237154589,
0.441434262690624));
#170469=CARTESIAN_POINT('Ctrl Pts',(19.7702742054051,-20.7980294610899,
0.445807834770614));
#170470=CARTESIAN_POINT('Ctrl Pts',(19.7066660505843,-20.8337360906338,
0.450181515120482));
#170471=CARTESIAN_POINT('Ctrl Pts',(19.6412144536897,-20.8661489951701,
0.454555195470349));
#170472=CARTESIAN_POINT('Ctrl Pts',(19.5742967209256,-20.8950878572009,
0.458928875820217));
#170473=CARTESIAN_POINT('Ctrl Pts',(19.5073097608989,-20.92405665686,0.463307080799151));
#170474=CARTESIAN_POINT('Ctrl Pts',(19.4388540801552,-20.949544046669,0.467685285778084));
#170475=CARTESIAN_POINT('Ctrl Pts',(19.3693269154526,-20.9714179137815,
0.472063490757018));
#170476=CARTESIAN_POINT('Ctrl Pts',(19.2997618805805,-20.9933036951876,
0.476444080463786));
#170477=CARTESIAN_POINT('Ctrl Pts',(19.2291246668025,-21.0115719142762,
0.480824670170555));
#170478=CARTESIAN_POINT('Ctrl Pts',(19.1578249890647,-21.0261411183052,
0.485205259877324));
#170479=CARTESIAN_POINT('Ctrl Pts',(19.0863993186969,-21.0407360673641,
0.489593590460847));
#170480=CARTESIAN_POINT('Ctrl Pts',(19.0143093237696,-21.0516188761684,
0.493981921044371));
#170481=CARTESIAN_POINT('Ctrl Pts',(18.9419715779474,-21.0587597923746,
0.498370251627894));
#170482=CARTESIAN_POINT('Ctrl Pts',(18.892967495442,-21.0635972951603,0.50134305803113));
#170483=CARTESIAN_POINT('Ctrl Pts',(18.843849807491,-21.0667186668706,0.504315864434366));
#170484=CARTESIAN_POINT('Ctrl Pts',(18.7947475334652,-21.0681282421389,
0.507288670837602));
#170485=CARTESIAN_POINT('Ctrl Pts',(18.7222522711166,-21.0702093581544,
0.511677762471143));
#170486=CARTESIAN_POINT('Ctrl Pts',(18.6495091063873,-21.0685648466706,
0.516066854104684));
#170487=CARTESIAN_POINT('Ctrl Pts',(18.5769328970345,-21.0631653002941,
0.520455945738226));
#170488=CARTESIAN_POINT('Ctrl Pts',(18.5044640538338,-21.0577737417766,
0.524838544336597));
#170489=CARTESIAN_POINT('Ctrl Pts',(18.4321621525778,-21.0486382115291,
0.529221142934969));
#170490=CARTESIAN_POINT('Ctrl Pts',(18.3604434250555,-21.0357812949817,
0.533603741533341));
#170491=CARTESIAN_POINT('Ctrl Pts',(18.2888085422895,-21.0229394091672,
0.537981216533957));
#170492=CARTESIAN_POINT('Ctrl Pts',(18.2177559511463,-21.0063848642472,
0.542358691534574));
#170493=CARTESIAN_POINT('Ctrl Pts',(18.1476964269544,-20.9861920067275,
0.54673616653519));
#170494=CARTESIAN_POINT('Ctrl Pts',(18.0776810830246,-20.966011883033,0.551110881054699));
#170495=CARTESIAN_POINT('Ctrl Pts',(18.0086580256524,-20.9421981323211,
0.555485595574208));
#170496=CARTESIAN_POINT('Ctrl Pts',(17.9410261110428,-20.9148758013262,
0.559860310093717));
#170497=CARTESIAN_POINT('Ctrl Pts',(17.8734145608305,-20.8875616972581,
0.564233707359009));
#170498=CARTESIAN_POINT('Ctrl Pts',(17.8071937685407,-20.8567412908305,
0.568607104624301));
#170499=CARTESIAN_POINT('Ctrl Pts',(17.742744149092,-20.8225883668089,0.572980501889593));
#170500=CARTESIAN_POINT('Ctrl Pts',(17.6782926999987,-20.7884344732282,
0.577354023310199));
#170501=CARTESIAN_POINT('Ctrl Pts',(17.6156129486706,-20.7509481017458,
0.581727544730805));
#170502=CARTESIAN_POINT('Ctrl Pts',(17.5550606677984,-20.7103489559778,
0.58610106615141));
#170503=CARTESIAN_POINT('Ctrl Pts',(17.4944453857489,-20.6697075691258,
0.590479137970356));
#170504=CARTESIAN_POINT('Ctrl Pts',(17.4359623948805,-20.6259472108894,
0.594857209789301));
#170505=CARTESIAN_POINT('Ctrl Pts',(17.3799377143115,-20.5793304294076,
0.599235281608247));
#170506=CARTESIAN_POINT('Ctrl Pts',(17.3238823352031,-20.5326881044139,
0.603615752377234));
#170507=CARTESIAN_POINT('Ctrl Pts',(17.2702883027459,-20.4831865672914,
0.607996223146221));
#170508=CARTESIAN_POINT('Ctrl Pts',(17.2194457820157,-20.4311262693854,
0.612376693915207));
#170509=CARTESIAN_POINT('Ctrl Pts',(17.1685131321094,-20.3789736835344,
0.616764929999832));
#170510=CARTESIAN_POINT('Ctrl Pts',(17.1203420532452,-20.3242536410108,
0.621153166084457));
#170511=CARTESIAN_POINT('Ctrl Pts',(17.0751829425931,-20.2673003345457,
0.625541402169081));
#170512=CARTESIAN_POINT('Ctrl Pts',(17.0445739735742,-20.228697227267,0.628515760619066));
#170513=CARTESIAN_POINT('Ctrl Pts',(17.0153478864754,-20.1890687880074,
0.631490119069051));
#170514=CARTESIAN_POINT('Ctrl Pts',(16.987570942693,-20.1485260330615,0.634464477519036));
#170515=CARTESIAN_POINT('Ctrl Pts',(16.9460128045002,-20.0878684810299,
0.638914527908589));
#170516=CARTESIAN_POINT('Ctrl Pts',(16.9075409804496,-20.0249304000689,
0.643364578298142));
#170517=CARTESIAN_POINT('Ctrl Pts',(16.872410053225,-19.9600535055572,0.647814628687695));
#170518=CARTESIAN_POINT('Ctrl Pts',(16.8373354187658,-19.8952805678748,
0.652257548447269));
#170519=CARTESIAN_POINT('Ctrl Pts',(16.8055912687537,-19.828575391364,0.656700468206843));
#170520=CARTESIAN_POINT('Ctrl Pts',(16.7773892711312,-19.7603090100176,
0.661143387966416));
#170521=CARTESIAN_POINT('Ctrl Pts',(16.7492305789296,-19.692147454734,0.665579485425226));
#170522=CARTESIAN_POINT('Ctrl Pts',(16.7246033993889,-19.6224298886478,
0.670015582884037));
#170523=CARTESIAN_POINT('Ctrl Pts',(16.703672960778,-19.5515507599895,0.674451680342847));
#170524=CARTESIAN_POINT('Ctrl Pts',(16.6827615111997,-19.4807359360554,
0.6788837531751));
#170525=CARTESIAN_POINT('Ctrl Pts',(16.6655402725696,-19.4087620863505,
0.683315826007353));
#170526=CARTESIAN_POINT('Ctrl Pts',(16.6521255619375,-19.3360414354493,
0.687747898839606));
#170527=CARTESIAN_POINT('Ctrl Pts',(16.6387183935307,-19.2633616706726,
0.6921774798036));
#170528=CARTESIAN_POINT('Ctrl Pts',(16.6291135877664,-19.1899363945333,
0.696607060767594));
#170529=CARTESIAN_POINT('Ctrl Pts',(16.6233766675227,-19.1161893675075,
0.701036641731588));
#170530=CARTESIAN_POINT('Ctrl Pts',(16.6190996547199,-19.0612091751119,
0.704339001480227));
#170531=CARTESIAN_POINT('Ctrl Pts',(16.6169713924744,-19.0060504437676,
0.707641361228867));
#170532=CARTESIAN_POINT('Ctrl Pts',(16.6170002905271,-18.9508909049915,
0.710943720977506));
#170533=CARTESIAN_POINT('',(20.3539256943887,-17.5890877707427,0.));
#170534=CARTESIAN_POINT('Origin',(18.734,-18.952,0.));
#170535=CARTESIAN_POINT('',(16.6170006157907,-18.95038529957,0.489056278967188));
#170536=CARTESIAN_POINT('Ctrl Pts',(16.6170006157907,-18.95038529957,0.489056278967188));
#170537=CARTESIAN_POINT('Ctrl Pts',(16.6169439873006,-19.0246297083089,
0.484575909845401));
#170538=CARTESIAN_POINT('Ctrl Pts',(16.6207979226554,-19.0990186013218,
0.480095540723614));
#170539=CARTESIAN_POINT('Ctrl Pts',(16.6285774659328,-19.1730994189093,
0.475615171601827));
#170540=CARTESIAN_POINT('Ctrl Pts',(16.6360763306427,-19.2445074706266,
0.471296449962676));
#170541=CARTESIAN_POINT('Ctrl Pts',(16.6472223424282,-19.3156287493154,
0.466977728323525));
#170542=CARTESIAN_POINT('Ctrl Pts',(16.661976057202,-19.3860573469854,0.462659006684374));
#170543=CARTESIAN_POINT('Ctrl Pts',(16.6767199431933,-19.4564390258024,
0.458343162135962));
#170544=CARTESIAN_POINT('Ctrl Pts',(16.6950666659208,-19.5261284537002,
0.45402731758755));
#170545=CARTESIAN_POINT('Ctrl Pts',(16.7169252820585,-19.5947274556461,
0.449711473039138));
#170546=CARTESIAN_POINT('Ctrl Pts',(16.7387770070935,-19.6633048312107,
0.445396989095061));
#170547=CARTESIAN_POINT('Ctrl Pts',(16.7641382780629,-19.7307919900002,
0.441082505150984));
#170548=CARTESIAN_POINT('Ctrl Pts',(16.7928681311363,-19.7968053430712,
0.436768021206907));
#170549=CARTESIAN_POINT('Ctrl Pts',(16.8215990084979,-19.8628210496769,
0.432453383441104));
#170550=CARTESIAN_POINT('Ctrl Pts',(16.8536985050873,-19.9273623922351,
0.428138745675302));
#170551=CARTESIAN_POINT('Ctrl Pts',(16.8889780480199,-19.9900669519407,
0.4238241079095));
#170552=CARTESIAN_POINT('Ctrl Pts',(16.9242924792532,-20.0528335208266,
0.419505203354288));
#170553=CARTESIAN_POINT('Ctrl Pts',(16.9627929852641,-20.1137592505177,
0.415186298799076));
#170554=CARTESIAN_POINT('Ctrl Pts',(17.0042462475466,-20.1725084825078,
0.410867394243864));
#170555=CARTESIAN_POINT('Ctrl Pts',(17.0457241648865,-20.2312926566376,
0.406545920944149));
#170556=CARTESIAN_POINT('Ctrl Pts',(17.0901580230918,-20.287897369665,0.402224447644434));
#170557=CARTESIAN_POINT('Ctrl Pts',(17.1372743346935,-20.3420201976056,
0.397902974344718));
#170558=CARTESIAN_POINT('Ctrl Pts',(17.1844652344071,-20.3962287054183,
0.393574659878474));
#170559=CARTESIAN_POINT('Ctrl Pts',(17.2343467098505,-20.4479471389023,
0.389246345412231));
#170560=CARTESIAN_POINT('Ctrl Pts',(17.2866094096999,-20.4969108320906,
0.384918030945987));
#170561=CARTESIAN_POINT('Ctrl Pts',(17.3002561753745,-20.5096961655967,
0.383787827312092));
#170562=CARTESIAN_POINT('Ctrl Pts',(17.3140651344993,-20.5222938940567,
0.382657623678198));
#170563=CARTESIAN_POINT('Ctrl Pts',(17.328030443818,-20.5346997842577,0.381527420044303));
#170564=CARTESIAN_POINT('Ctrl Pts',(17.3823195205318,-20.5829267378796,
0.377133839466686));
#170565=CARTESIAN_POINT('Ctrl Pts',(17.4391958931759,-20.628448704409,0.372740258889068));
#170566=CARTESIAN_POINT('Ctrl Pts',(17.498359246263,-20.6709767094712,0.368346678311451));
#170567=CARTESIAN_POINT('Ctrl Pts',(17.5574363013708,-20.7134426815229,
0.363959506382193));
#170568=CARTESIAN_POINT('Ctrl Pts',(17.6187933267003,-20.7529230838071,
0.359572334452935));
#170569=CARTESIAN_POINT('Ctrl Pts',(17.6820956518213,-20.7891679951172,
0.355185162523678));
#170570=CARTESIAN_POINT('Ctrl Pts',(17.7453255105041,-20.8253714144342,
0.350803012885832));
#170571=CARTESIAN_POINT('Ctrl Pts',(17.8104958295947,-20.8583464631661,
0.346420863247986));
#170572=CARTESIAN_POINT('Ctrl Pts',(17.8772429582996,-20.8878864562512,
0.342038713610141));
#170573=CARTESIAN_POINT('Ctrl Pts',(17.9439489461201,-20.9174082417899,
0.33765926499503));
#170574=CARTESIAN_POINT('Ctrl Pts',(18.0122293762549,-20.9434989788705,
0.33327981637992));
#170575=CARTESIAN_POINT('Ctrl Pts',(18.081697252437,-20.9659985415888,0.32890036776481));
#170576=CARTESIAN_POINT('Ctrl Pts',(18.1511450535803,-20.9884916023148,
0.324522184736119));
#170577=CARTESIAN_POINT('Ctrl Pts',(18.2217791621869,-21.0073954011508,
0.320144001707428));
#170578=CARTESIAN_POINT('Ctrl Pts',(18.2931954849952,-21.0225990388174,
0.315765818678737));
#170579=CARTESIAN_POINT('Ctrl Pts',(18.3646145496345,-21.0378032601853,
0.311387467561894));
#170580=CARTESIAN_POINT('Ctrl Pts',(18.4368154173397,-21.0493069401342,
0.307009116445052));
#170581=CARTESIAN_POINT('Ctrl Pts',(18.5093834475756,-21.0570502142175,
0.302630765328209));
#170582=CARTESIAN_POINT('Ctrl Pts',(18.5820274277171,-21.0648015924333,
0.298247831816703));
#170583=CARTESIAN_POINT('Ctrl Pts',(18.6550388584148,-21.0687846559847,
0.293864898305197));
#170584=CARTESIAN_POINT('Ctrl Pts',(18.7279984288039,-21.0689914929312,
0.289481964793692));
#170585=CARTESIAN_POINT('Ctrl Pts',(18.8009983528725,-21.0691984442785,
0.285096607097214));
#170586=CARTESIAN_POINT('Ctrl Pts',(18.8739458788801,-21.0656250338833,
0.280711249400737));
#170587=CARTESIAN_POINT('Ctrl Pts',(18.946424858768,-21.0583154273227,0.27632589170426));
#170588=CARTESIAN_POINT('Ctrl Pts',(19.0190319251111,-21.0509929030637,
0.271932784106734));
#170589=CARTESIAN_POINT('Ctrl Pts',(19.091168316046,-21.0399210701979,0.267539676509208));
#170590=CARTESIAN_POINT('Ctrl Pts',(19.1624267103003,-21.0251954934114,
0.263146568911682));
#170591=CARTESIAN_POINT('Ctrl Pts',(19.2099795641009,-21.0153686764113,
0.260214917062078));
#170592=CARTESIAN_POINT('Ctrl Pts',(19.2571416600211,-21.003915800001,0.257283265212473));
#170593=CARTESIAN_POINT('Ctrl Pts',(19.3037962227791,-20.9908774520571,
0.254351613362869));
#170594=CARTESIAN_POINT('Ctrl Pts',(19.3728933262966,-20.971567184758,0.250009730396774));
#170595=CARTESIAN_POINT('Ctrl Pts',(19.4411588243116,-20.9486979955926,
0.245667847430679));
#170596=CARTESIAN_POINT('Ctrl Pts',(19.5081940324577,-20.9223584953269,
0.241325964464583));
#170597=CARTESIAN_POINT('Ctrl Pts',(19.5751282952576,-20.8960586585461,
0.236990619747436));
#170598=CARTESIAN_POINT('Ctrl Pts',(19.6408354886486,-20.8662990562217,
0.232655275030289));
#170599=CARTESIAN_POINT('Ctrl Pts',(19.7049304077652,-20.833218526189,0.228319930313142));
#170600=CARTESIAN_POINT('Ctrl Pts',(19.7689516598175,-20.8001760170412,
0.223989568395299));
#170601=CARTESIAN_POINT('Ctrl Pts',(19.8313638797399,-20.7638203813565,
0.219659206477455));
#170602=CARTESIAN_POINT('Ctrl Pts',(19.8918019327492,-20.7243384791067,
0.215328844559612));
#170603=CARTESIAN_POINT('Ctrl Pts',(19.952202841651,-20.6848808417024,0.211001144001965));
#170604=CARTESIAN_POINT('Ctrl Pts',(20.0106315769706,-20.6423010159659,
0.206673443444318));
#170605=CARTESIAN_POINT('Ctrl Pts',(20.0667491221407,-20.5968309267013,
0.202345742886671));
#170606=CARTESIAN_POINT('Ctrl Pts',(20.1228516204485,-20.5513730293844,
0.198019202720377));
#170607=CARTESIAN_POINT('Ctrl Pts',(20.1766437747633,-20.5030267163447,
0.193692662554083));
#170608=CARTESIAN_POINT('Ctrl Pts',(20.2278184819436,-20.4520651129214,
0.189366122387789));
#170609=CARTESIAN_POINT('Ctrl Pts',(20.2789971971884,-20.401099518124,0.18503924336167));
#170610=CARTESIAN_POINT('Ctrl Pts',(20.3275577103422,-20.3475185761416,
0.180712364335552));
#170611=CARTESIAN_POINT('Ctrl Pts',(20.3732300428321,-20.2916319892705,
0.176385485309434));
#170612=CARTESIAN_POINT('Ctrl Pts',(20.4189571873855,-20.2356783320532,
0.172053413529732));
#170613=CARTESIAN_POINT('Ctrl Pts',(20.461788919467,-20.1774138895481,0.167721341750031));
#170614=CARTESIAN_POINT('Ctrl Pts',(20.5014963977798,-20.11718045119,0.163389269970329));
#170615=CARTESIAN_POINT('Ctrl Pts',(20.5412283831299,-20.0569098373883,
0.159054524481558));
#170616=CARTESIAN_POINT('Ctrl Pts',(20.5778320305151,-19.994668236685,0.154719778992786));
#170617=CARTESIAN_POINT('Ctrl Pts',(20.6111241303052,-19.9308227620085,
0.150385033504014));
#170618=CARTESIAN_POINT('Ctrl Pts',(20.6444832806256,-19.8668487020833,
0.146041557806415));
#170619=CARTESIAN_POINT('Ctrl Pts',(20.6745173629453,-19.8012647680478,
0.141698082108817));
#170620=CARTESIAN_POINT('Ctrl Pts',(20.7010912717234,-19.7344582600432,
0.137354606411219));
#170621=CARTESIAN_POINT('Ctrl Pts',(20.721849646991,-19.6822719379232,0.133961673167958));
#170622=CARTESIAN_POINT('Ctrl Pts',(20.7404975804328,-19.6293400279684,
0.130568739924696));
#170623=CARTESIAN_POINT('Ctrl Pts',(20.7569922863659,-19.5758519129603,
0.127175806681435));
#170624=CARTESIAN_POINT('Ctrl Pts',(20.7789195445138,-19.5047474197739,
0.12266540659273));
#170625=CARTESIAN_POINT('Ctrl Pts',(20.7971288584811,-19.4323721967961,
0.118155006504025));
#170626=CARTESIAN_POINT('Ctrl Pts',(20.8114809541406,-19.3591386559676,
0.113644606415321));
#170627=CARTESIAN_POINT('Ctrl Pts',(20.8265483375802,-19.2822552609233,
0.108909414481349));
#170628=CARTESIAN_POINT('Ctrl Pts',(20.8373637838653,-19.2044262083738,
0.104174222547377));
#170629=CARTESIAN_POINT('Ctrl Pts',(20.8438249724136,-19.1261481719107,
0.0994390306134055));
#170630=CARTESIAN_POINT('Ctrl Pts',(20.8499589701725,-19.0518340891932,
0.0949436260150769));
#170631=CARTESIAN_POINT('Ctrl Pts',(20.852168892667,-18.9771159048155,0.0904482214167483));
#170632=CARTESIAN_POINT('Ctrl Pts',(20.8504195396485,-18.9024285143068,
0.0859528168184197));
#170633=CARTESIAN_POINT('Ctrl Pts',(20.848671831534,-18.8278113518075,0.0814616392162973));
#170634=CARTESIAN_POINT('Ctrl Pts',(20.842972258343,-18.7532253737159,0.0769704616141749));
#170635=CARTESIAN_POINT('Ctrl Pts',(20.833337630623,-18.6791071407126,0.0724792840120526));
#170636=CARTESIAN_POINT('Ctrl Pts',(20.8237095451823,-18.6050392368129,
0.067991156090602));
#170637=CARTESIAN_POINT('Ctrl Pts',(20.810151776091,-18.5314388917089,0.0635030281691514));
#170638=CARTESIAN_POINT('Ctrl Pts',(20.7927329926196,-18.4587379346641,
0.0590149002477008));
#170639=CARTESIAN_POINT('Ctrl Pts',(20.775321490724,-18.3860673688074,0.0545286484988));
#170640=CARTESIAN_POINT('Ctrl Pts',(20.7540522902898,-18.3142958801147,
0.0500423967498992));
#170641=CARTESIAN_POINT('Ctrl Pts',(20.7290449663564,-18.2438442387327,
0.0455561450009983));
#170642=CARTESIAN_POINT('Ctrl Pts',(20.704034536135,-18.1733838461909,0.0410693359917531));
#170643=CARTESIAN_POINT('Ctrl Pts',(20.6752851982857,-18.1042440551513,
0.0365825269825079));
#170644=CARTESIAN_POINT('Ctrl Pts',(20.6429658444502,-18.0368287566131,
0.0320957179732627));
#170645=CARTESIAN_POINT('Ctrl Pts',(20.610644937254,-17.9694102179022,0.0276086933151065));
#170646=CARTESIAN_POINT('Ctrl Pts',(20.5747538739462,-17.9037167392705,
0.0231216686569502));
#170647=CARTESIAN_POINT('Ctrl Pts',(20.5355082322583,-17.8401290141812,
0.018634643998794));
#170648=CARTESIAN_POINT('Ctrl Pts',(20.496235508383,-17.7764974091956,0.0141445229855435));
#170649=CARTESIAN_POINT('Ctrl Pts',(20.4536038273032,-17.7149748381304,
0.00965440197229298));
#170650=CARTESIAN_POINT('Ctrl Pts',(20.4078725225403,-17.6559136686608,
0.0051642809590425));
#170651=CARTESIAN_POINT('Ctrl Pts',(20.3903400101855,-17.6332707397352,
0.003442853972695));
#170652=CARTESIAN_POINT('Ctrl Pts',(20.3723523439628,-17.6109892567414,
0.0017214269863475));
#170653=CARTESIAN_POINT('Ctrl Pts',(20.3539256943887,-17.5890877707427,
0.));
#170654=CARTESIAN_POINT('Ctrl Pts',(16.6170005688548,-18.9504480557866,
0.490010467130569));
#170655=CARTESIAN_POINT('Ctrl Pts',(16.6170514726509,-18.881010439057,0.494577327914728));
#170656=CARTESIAN_POINT('Ctrl Pts',(16.6205187004332,-18.8116103989348,
0.4990989912545));
#170657=CARTESIAN_POINT('Ctrl Pts',(16.6297024906936,-18.7192634938256,
0.504962249724503));
#170658=CARTESIAN_POINT('Ctrl Pts',(16.6323977830403,-18.696065413783,0.506421957048484));
#170659=CARTESIAN_POINT('Ctrl Pts',(16.6362852621,-18.6668342307142,0.508240701531616));
#170660=CARTESIAN_POINT('Ctrl Pts',(16.6371204756518,-18.6607562875839,
0.508617738798077));
#170661=CARTESIAN_POINT('Ctrl Pts',(16.6385603498371,-18.6506055337555,
0.509245444537397));
#170662=CARTESIAN_POINT('Ctrl Pts',(16.6391504857804,-18.646530745929,0.509496887875124));
#170663=CARTESIAN_POINT('Ctrl Pts',(16.640246229322,-18.6391173555341,0.509953340961934));
#170664=CARTESIAN_POINT('Ctrl Pts',(16.6407479422945,-18.635778203287,0.510158565565758));
#170665=CARTESIAN_POINT('Ctrl Pts',(16.6417945762328,-18.628923976198,0.510579043266343));
#170666=CARTESIAN_POINT('Ctrl Pts',(16.6423403650127,-18.6254090872902,
0.510794240062932));
#170667=CARTESIAN_POINT('Ctrl Pts',(16.6435932922711,-18.6174721992057,
0.51127920709439));
#170668=CARTESIAN_POINT('Ctrl Pts',(16.644305601679,-18.6130510721356,0.511548680018681));
#170669=CARTESIAN_POINT('Ctrl Pts',(16.6465009453004,-18.5996951238187,
0.512360802943133));
#170670=CARTESIAN_POINT('Ctrl Pts',(16.6480273156697,-18.5907673934348,
0.51290103930551));
#170671=CARTESIAN_POINT('Ctrl Pts',(16.6601810646459,-18.5223272731401,
0.517024246191999));
#170672=CARTESIAN_POINT('Ctrl Pts',(16.6732969949638,-18.4632790241335,
0.520475810165007));
#170673=CARTESIAN_POINT('Ctrl Pts',(16.6938140193657,-18.3865902843641,
0.524913687944728));
#170674=CARTESIAN_POINT('Ctrl Pts',(16.6989488457143,-18.3683787117175,
0.525964161652573));
#170675=CARTESIAN_POINT('Ctrl Pts',(16.7159637402776,-18.3109894546689,
0.529270380732414));
#170676=CARTESIAN_POINT('Ctrl Pts',(16.7287365520966,-18.2720856477678,
0.531505691843595));
#170677=CARTESIAN_POINT('Ctrl Pts',(16.7435546348056,-18.2310120132186,
0.533880985320879));
#170678=CARTESIAN_POINT('Ctrl Pts',(16.7444845345614,-18.2284499731407,
0.53402921203008));
#170679=CARTESIAN_POINT('Ctrl Pts',(16.7454193692601,-18.2258897638472,
0.53417740218321));
#170680=CARTESIAN_POINT('Origin',(18.734,-18.952,0.));
#170681=CARTESIAN_POINT('',(16.7454191832631,-18.2258902732327,1.55576066005867));
#170682=CARTESIAN_POINT('',(16.7454193692336,-18.2258897639197,1.33163196665472));
#170683=CARTESIAN_POINT('',(16.7454193692319,-18.2258897639242,0.));
#170684=CARTESIAN_POINT('',(16.6170003908423,-18.9507135995066,1.51094372094299));
#170685=CARTESIAN_POINT('Ctrl Pts',(16.7454191832631,-18.2258902732327,
1.55576066005867));
#170686=CARTESIAN_POINT('Ctrl Pts',(16.7161439153024,-18.3060658088651,
1.55013147756805));
#170687=CARTESIAN_POINT('Ctrl Pts',(16.6917244024261,-18.3879928335124,
1.54446140094733));
#170688=CARTESIAN_POINT('Ctrl Pts',(16.66602267378,-18.4982088831121,1.53708123670477));
#170689=CARTESIAN_POINT('Ctrl Pts',(16.6602607693149,-18.5253124031872,
1.53528610611094));
#170690=CARTESIAN_POINT('Ctrl Pts',(16.6468711293343,-18.5949949214027,
1.53073310070744));
#170691=CARTESIAN_POINT('Ctrl Pts',(16.6400127044978,-18.6377113678681,
1.52800094154312));
#170692=CARTESIAN_POINT('Ctrl Pts',(16.6335056815886,-18.6880513304626,
1.52487274099519));
#170693=CARTESIAN_POINT('Ctrl Pts',(16.6325834866175,-18.69549673892,1.52441241354194));
#170694=CARTESIAN_POINT('Ctrl Pts',(16.6311572000861,-18.7075362692343,
1.52367199847394));
#170695=CARTESIAN_POINT('Ctrl Pts',(16.6306285482168,-18.712127338848,1.52339058146462));
#170696=CARTESIAN_POINT('Ctrl Pts',(16.6297175154369,-18.7202738430539,
1.52289291772099));
#170697=CARTESIAN_POINT('Ctrl Pts',(16.6293291050042,-18.723828548914,1.52267633544412));
#170698=CARTESIAN_POINT('Ctrl Pts',(16.628593654091,-18.7307210376584,1.5222575051168));
#170699=CARTESIAN_POINT('Ctrl Pts',(16.6282455448752,-18.7340586417142,
1.52205519562351));
#170700=CARTESIAN_POINT('Ctrl Pts',(16.6274962875417,-18.7414117890565,
1.52161056542226));
#170701=CARTESIAN_POINT('Ctrl Pts',(16.6270986812446,-18.7454276910519,
1.52136844218618));
#170702=CARTESIAN_POINT('Ctrl Pts',(16.6261439823156,-18.7553599193906,
1.52077131891836));
#170703=CARTESIAN_POINT('Ctrl Pts',(16.6256003086776,-18.7612775417385,
1.52041704492448));
#170704=CARTESIAN_POINT('Ctrl Pts',(16.6234160973003,-18.7862031920286,
1.51893079183033));
#170705=CARTESIAN_POINT('Ctrl Pts',(16.6220075766885,-18.8052313011762,
1.51781084192716));
#170706=CARTESIAN_POINT('Ctrl Pts',(16.6183136906642,-18.8663454677846,
1.51425337207207));
#170707=CARTESIAN_POINT('Ctrl Pts',(16.6170276587882,-18.9084831004558,
1.51186056911543));
#170708=CARTESIAN_POINT('Ctrl Pts',(16.617000441359,-18.9506329908568,1.50950272412443));
#170709=CARTESIAN_POINT('Ctrl Pts',(16.7454193692319,-18.2258897639242,
0.755484063719885));
#170710=CARTESIAN_POINT('Ctrl Pts',(16.7570609226712,-18.1940073216569,
0.757536137213414));
#170711=CARTESIAN_POINT('Ctrl Pts',(16.7694632458252,-18.1624216014919,
0.759588210706942));
#170712=CARTESIAN_POINT('Ctrl Pts',(16.7826102689518,-18.1311668150229,
0.761640284200471));
#170713=CARTESIAN_POINT('Ctrl Pts',(16.8107255694665,-18.0643275232961,
0.766028704483401));
#170714=CARTESIAN_POINT('Ctrl Pts',(16.8423337670678,-17.9988040424724,
0.770417124766331));
#170715=CARTESIAN_POINT('Ctrl Pts',(16.8772900689618,-17.9349861200633,
0.774805545049261));
#170716=CARTESIAN_POINT('Ctrl Pts',(16.9121945047598,-17.8712628869177,
0.779187454053404));
#170717=CARTESIAN_POINT('Ctrl Pts',(16.9504369534201,-17.8092406080986,
0.783569363057546));
#170718=CARTESIAN_POINT('Ctrl Pts',(16.9918247170348,-17.7492887780415,
0.787951272061689));
#170719=CARTESIAN_POINT('Ctrl Pts',(17.0331638610962,-17.6894073753507,
0.792328033494681));
#170720=CARTESIAN_POINT('Ctrl Pts',(17.0776407074798,-17.6315919847378,
0.796704794927673));
#170721=CARTESIAN_POINT('Ctrl Pts',(17.1250176914327,-17.5761857208484,
0.801081556360666));
#170722=CARTESIAN_POINT('Ctrl Pts',(17.1723646383057,-17.5208145846146,
0.805455542920259));
#170723=CARTESIAN_POINT('Ctrl Pts',(17.2226077618452,-17.4678499102326,
0.809829529479853));
#170724=CARTESIAN_POINT('Ctrl Pts',(17.2754682696248,-17.4176029876565,
0.814203516039446));
#170725=CARTESIAN_POINT('Ctrl Pts',(17.328312696826,-17.3673713505858,0.818576171998238));
#170726=CARTESIAN_POINT('Ctrl Pts',(17.3837725781244,-17.319856156042,0.82294882795703));
#170727=CARTESIAN_POINT('Ctrl Pts',(17.4415323794237,-17.2753317412911,
0.827321483915821));
#170728=CARTESIAN_POINT('Ctrl Pts',(17.499293658057,-17.2308061877305,0.831694251714908));
#170729=CARTESIAN_POINT('Ctrl Pts',(17.5593545902617,-17.1892718587225,
0.836067019513995));
#170730=CARTESIAN_POINT('Ctrl Pts',(17.6213680340651,-17.1509616582705,
0.840439787313082));
#170731=CARTESIAN_POINT('Ctrl Pts',(17.6834458140768,-17.112611712678,0.844817091665573));
#170732=CARTESIAN_POINT('Ctrl Pts',(17.7474797388099,-17.0774928279821,
0.849194396018063));
#170733=CARTESIAN_POINT('Ctrl Pts',(17.8130959747628,-17.0457930919489,
0.853571700370554));
#170734=CARTESIAN_POINT('Ctrl Pts',(17.8787480372569,-17.0140760478229,
0.857951394736325));
#170735=CARTESIAN_POINT('Ctrl Pts',(17.9459836862096,-16.9857820564869,
0.862331089102096));
#170736=CARTESIAN_POINT('Ctrl Pts',(18.0144094204716,-16.9610508801443,
0.866710783467866));
#170737=CARTESIAN_POINT('Ctrl Pts',(18.0829563836852,-16.9362758879098,
0.871098237279143));
#170738=CARTESIAN_POINT('Ctrl Pts',(18.1526971808355,-16.9150764562721,
0.87548569109042));
#170739=CARTESIAN_POINT('Ctrl Pts',(18.2232240532573,-16.8975421804697,
0.879873144901697));
#170740=CARTESIAN_POINT('Ctrl Pts',(18.2711423552575,-16.8856288105101,
0.882854126895099));
#170741=CARTESIAN_POINT('Ctrl Pts',(18.3194232835352,-16.8754063197374,
0.885835108888502));
#170742=CARTESIAN_POINT('Ctrl Pts',(18.3679374540643,-16.8668891606288,
0.888816090881905));
#170743=CARTESIAN_POINT('Ctrl Pts',(18.4393551942814,-16.8543510454768,
0.893204396304316));
#170744=CARTESIAN_POINT('Ctrl Pts',(18.5115571786451,-16.8454619390755,
0.897592701726727));
#170745=CARTESIAN_POINT('Ctrl Pts',(18.5841373366349,-16.8403110593345,
0.901981007149137));
#170746=CARTESIAN_POINT('Ctrl Pts',(18.6566098160556,-16.8351678213426,
0.906362802163441));
#170747=CARTESIAN_POINT('Ctrl Pts',(18.7294588781678,-16.8337518343611,
0.910744597177744));
#170748=CARTESIAN_POINT('Ctrl Pts',(18.8022695511268,-16.8361010732105,
0.915126392192048));
#170749=CARTESIAN_POINT('Ctrl Pts',(18.8749947199703,-16.8384475532667,
0.919503041511469));
#170750=CARTESIAN_POINT('Ctrl Pts',(18.9476811095042,-16.8445504600611,
0.92387969083089));
#170751=CARTESIAN_POINT('Ctrl Pts',(19.0199116428383,-16.8543957636176,
0.928256340150311));
#170752=CARTESIAN_POINT('Ctrl Pts',(19.0920964007967,-16.8642348278118,
0.932630215812144));
#170753=CARTESIAN_POINT('Ctrl Pts',(19.1638253990005,-16.8778115180026,
0.937004091473978));
#170754=CARTESIAN_POINT('Ctrl Pts',(19.2346860042546,-16.8950599121162,
0.941377967135811));
#170755=CARTESIAN_POINT('Ctrl Pts',(19.3055250750244,-16.9123030644558,
0.945750513580145));
#170756=CARTESIAN_POINT('Ctrl Pts',(19.3754958083888,-16.9332155914393,
0.950123060024478));
#170757=CARTESIAN_POINT('Ctrl Pts',(19.4441967552487,-16.9576806753094,
0.954495606468812));
#170758=CARTESIAN_POINT('Ctrl Pts',(19.512899483717,-16.9821463936279,0.958868266305556));
#170759=CARTESIAN_POINT('Ctrl Pts',(19.5803319065734,-17.0101646880441,
0.9632409261423));
#170760=CARTESIAN_POINT('Ctrl Pts',(19.6461103054445,-17.0415697367603,
0.967613585979044));
#170761=CARTESIAN_POINT('Ctrl Pts',(19.7119569957736,-17.073007390353,0.971990785532794));
#170762=CARTESIAN_POINT('Ctrl Pts',(19.776145797365,-17.1078386101949,0.976367985086543));
#170763=CARTESIAN_POINT('Ctrl Pts',(19.8383162282127,-17.1458508732372,
0.980745184640292));
#170764=CARTESIAN_POINT('Ctrl Pts',(19.9005206278453,-17.1838839054839,
0.985124775815712));
#170765=CARTESIAN_POINT('Ctrl Pts',(19.9607040628243,-17.2251011686578,
0.989504366991133));
#170766=CARTESIAN_POINT('Ctrl Pts',(20.0185360408569,-17.2692474454811,
0.993883958166554));
#170767=CARTESIAN_POINT('Ctrl Pts',(20.0764705311577,-17.3134719754634,
0.99827131255258));
#170768=CARTESIAN_POINT('Ctrl Pts',(20.1320448727674,-17.3606355747934,
1.00265866693861));
#170769=CARTESIAN_POINT('Ctrl Pts',(20.1849630396155,-17.4104438843592,
1.00704602132463));
#170770=CARTESIAN_POINT('Ctrl Pts',(20.2209299975094,-17.4442971615911,
1.01002798007087));
#170771=CARTESIAN_POINT('Ctrl Pts',(20.2556706880075,-17.4793713845315,
1.0130099388171));
#170772=CARTESIAN_POINT('Ctrl Pts',(20.2891028481193,-17.5155654794696,
1.01599189756334));
#170773=CARTESIAN_POINT('Ctrl Pts',(20.3382999033156,-17.568826856554,1.02037999538716));
#170774=CARTESIAN_POINT('Ctrl Pts',(20.3848536164314,-17.6247226321812,
1.02476809321097));
#170775=CARTESIAN_POINT('Ctrl Pts',(20.4284691662198,-17.6829597150876,
1.02915619103479));
#170776=CARTESIAN_POINT('Ctrl Pts',(20.4720199640021,-17.741110338739,1.03353777425227));
#170777=CARTESIAN_POINT('Ctrl Pts',(20.5126409708618,-17.8015949865701,
1.03791935746975));
#170778=CARTESIAN_POINT('Ctrl Pts',(20.5500756303539,-17.8640853411987,
1.04230094068724));
#170779=CARTESIAN_POINT('Ctrl Pts',(20.5874662819946,-17.9265022327246,
1.04667737295463));
#170780=CARTESIAN_POINT('Ctrl Pts',(20.6216777807228,-17.9909197353098,
1.05105380522201));
#170781=CARTESIAN_POINT('Ctrl Pts',(20.6524961553591,-18.0569796081249,
1.0554302374894));
#170782=CARTESIAN_POINT('Ctrl Pts',(20.6832949761952,-18.1229975669334,
1.05980389297562));
#170783=CARTESIAN_POINT('Ctrl Pts',(20.7107047410892,-18.1906553922989,
1.06417754846184));
#170784=CARTESIAN_POINT('Ctrl Pts',(20.7345575147539,-18.2595704872252,
1.06855120394807));
#170785=CARTESIAN_POINT('Ctrl Pts',(20.7584030239131,-18.3284645936452,
1.07292352741122));
#170786=CARTESIAN_POINT('Ctrl Pts',(20.778693534838,-18.3986147538376,1.07729585087438));
#170787=CARTESIAN_POINT('Ctrl Pts',(20.7953099596495,-18.4696202219725,
1.08166817433753));
#170788=CARTESIAN_POINT('Ctrl Pts',(20.8119268059284,-18.5406274911261,
1.08604060870252));
#170789=CARTESIAN_POINT('Ctrl Pts',(20.8248692730975,-18.6124896411231,
1.0904130430675));
#170790=CARTESIAN_POINT('Ctrl Pts',(20.834069074416,-18.6847943064204,1.09478547743249));
#170791=CARTESIAN_POINT('Ctrl Pts',(20.8432784226837,-18.7571740047468,
1.09916244922245));
#170792=CARTESIAN_POINT('Ctrl Pts',(20.8487372896263,-18.8299966556521,
1.10353942101241));
#170793=CARTESIAN_POINT('Ctrl Pts',(20.8504292339814,-18.9028441504098,
1.10791639280238));
#170794=CARTESIAN_POINT('Ctrl Pts',(20.8521221021995,-18.9757314225439,
1.11229575457781));
#170795=CARTESIAN_POINT('Ctrl Pts',(20.8500439663687,-19.0486430829948,
1.11667511635325));
#170796=CARTESIAN_POINT('Ctrl Pts',(20.8442305173074,-19.1211631278514,
1.12105447812869));
#170797=CARTESIAN_POINT('Ctrl Pts',(20.8384067629935,-19.1938117258918,
1.12544160301156));
#170798=CARTESIAN_POINT('Ctrl Pts',(20.8288345361362,-19.2660668433993,
1.12982872789443));
#170799=CARTESIAN_POINT('Ctrl Pts',(20.8156010959129,-19.3375202685906,
1.1342158527773));
#170800=CARTESIAN_POINT('Ctrl Pts',(20.8066002282646,-19.3861200893717,
1.13719980326646));
#170801=CARTESIAN_POINT('Ctrl Pts',(20.7959066877834,-19.4343492460054,
1.14018375375562));
#170802=CARTESIAN_POINT('Ctrl Pts',(20.7835610200617,-19.482083601938,1.14316770424478));
#170803=CARTESIAN_POINT('Ctrl Pts',(20.7654052834301,-19.5522825100999,
1.14755594961346));
#170804=CARTESIAN_POINT('Ctrl Pts',(20.7436033966526,-19.6216845776909,
1.15194419498214));
#170805=CARTESIAN_POINT('Ctrl Pts',(20.7182422535391,-19.689883242302,1.15633244035082));
#170806=CARTESIAN_POINT('Ctrl Pts',(20.6929187482514,-19.7579806950138,
1.16071417323644));
#170807=CARTESIAN_POINT('Ctrl Pts',(20.6640466392656,-19.8248778416993,
1.16509590612206));
#170808=CARTESIAN_POINT('Ctrl Pts',(20.6317631511028,-19.8901812310617,
1.16947763900768));
#170809=CARTESIAN_POINT('Ctrl Pts',(20.5995175958008,-19.9554078894224,
1.17385422338941));
#170810=CARTESIAN_POINT('Ctrl Pts',(20.563868836638,-20.0190440802309,1.17823080777115));
#170811=CARTESIAN_POINT('Ctrl Pts',(20.5250023084886,-20.0807159655947,
1.18260739215288));
#170812=CARTESIAN_POINT('Ctrl Pts',(20.4861604270437,-20.1423487425328,
1.18698120118042));
#170813=CARTESIAN_POINT('Ctrl Pts',(20.4441050817949,-20.2020192784522,
1.19135501020796));
#170814=CARTESIAN_POINT('Ctrl Pts',(20.3990671042951,-20.2593792633335,
1.1957288192355));
#170815=CARTESIAN_POINT('Ctrl Pts',(20.3540428305095,-20.316721795281,1.20010129744332));
#170816=CARTESIAN_POINT('Ctrl Pts',(20.3060380239067,-20.3717547927606,
1.20447377565114));
#170817=CARTESIAN_POINT('Ctrl Pts',(20.2553252151259,-20.4241611969557,
1.20884625385896));
#170818=CARTESIAN_POINT('Ctrl Pts',(20.2046111087068,-20.4765689421249,
1.21321884394967));
#170819=CARTESIAN_POINT('Ctrl Pts',(20.1511891994121,-20.5263496153214,
1.21759143404038));
#170820=CARTESIAN_POINT('Ctrl Pts',(20.0953692846382,-20.5732225852251,
1.22196402413109));
#170821=CARTESIAN_POINT('Ctrl Pts',(20.0394914401257,-20.6201441997549,
1.22634115208255));
#170822=CARTESIAN_POINT('Ctrl Pts',(19.9812109915843,-20.6641517752805,
1.23071828003401));
#170823=CARTESIAN_POINT('Ctrl Pts',(19.9208706274007,-20.7050051665108,
1.23509540798547));
#170824=CARTESIAN_POINT('Ctrl Pts',(19.8604973096611,-20.7458808689175,
1.2394749264086));
#170825=CARTESIAN_POINT('Ctrl Pts',(19.7980622496215,-20.7835987077736,
1.24385444483173));
#170826=CARTESIAN_POINT('Ctrl Pts',(19.7339345832298,-20.817963512307,1.24823396325486));
#170827=CARTESIAN_POINT('Ctrl Pts',(19.6696932585229,-20.8523892241836,
1.25262124382984));
#170828=CARTESIAN_POINT('Ctrl Pts',(19.6037537734795,-20.8834498283967,
1.25700852440483));
#170829=CARTESIAN_POINT('Ctrl Pts',(19.5365066244677,-20.9109977329455,
1.26139580497982));
#170830=CARTESIAN_POINT('Ctrl Pts',(19.4907905516214,-20.9297253969375,
1.26437837362862));
#170831=CARTESIAN_POINT('Ctrl Pts',(19.4444705328526,-20.9468306580778,
1.26736094227741));
#170832=CARTESIAN_POINT('Ctrl Pts',(19.3976727118431,-20.9622804609195,
1.27034351092621));
#170833=CARTESIAN_POINT('Ctrl Pts',(19.3288196249197,-20.9850115752121,
1.27473172930904));
#170834=CARTESIAN_POINT('Ctrl Pts',(19.2586629672397,-21.0042455876802,
1.27911994769187));
#170835=CARTESIAN_POINT('Ctrl Pts',(19.1875916221637,-21.0198354964317,
1.2835081660747));
#170836=CARTESIAN_POINT('Ctrl Pts',(19.1166257539218,-21.0354022682323,
1.28788987191184));
#170837=CARTESIAN_POINT('Ctrl Pts',(19.044748360357,-21.0473355698463,1.29227157774898));
#170838=CARTESIAN_POINT('Ctrl Pts',(18.9723645439181,-21.0555378162046,
1.29665328358612));
#170839=CARTESIAN_POINT('Ctrl Pts',(18.9000657777863,-21.0637304250001,
1.30102984095989));
#170840=CARTESIAN_POINT('Ctrl Pts',(18.8272622477646,-21.0682006332517,
1.30540639833367));
#170841=CARTESIAN_POINT('Ctrl Pts',(18.7543686602251,-21.0689020094659,
1.30978295570745));
#170842=CARTESIAN_POINT('Ctrl Pts',(18.6815212968394,-21.069602940915,1.3141567377663));
#170843=CARTESIAN_POINT('Ctrl Pts',(18.6085844704128,-21.0665397776425,
1.31853051982516));
#170844=CARTESIAN_POINT('Ctrl Pts',(18.5359759950225,-21.0597180773179,
1.32290430188402));
#170845=CARTESIAN_POINT('Ctrl Pts',(18.4633896110466,-21.0528984525225,
1.32727675320246));
#170846=CARTESIAN_POINT('Ctrl Pts',(18.3911318597423,-21.0423226060684,
1.33164920452091));
#170847=CARTESIAN_POINT('Ctrl Pts',(18.3196168489478,-21.0280480736544,
1.33602165583936));
#170848=CARTESIAN_POINT('Ctrl Pts',(18.2481000062642,-21.0137731755918,
1.34039421916011));
#170849=CARTESIAN_POINT('Ctrl Pts',(18.1773264145167,-20.9957994998463,
1.34476678248086));
#170850=CARTESIAN_POINT('Ctrl Pts',(18.1076997236331,-20.9742356350887,
1.34913934580161));
#170851=CARTESIAN_POINT('Ctrl Pts',(18.0380007680099,-20.9526493894446,
1.35351644735541));
#170852=CARTESIAN_POINT('Ctrl Pts',(17.9694515516428,-20.927465658161,1.35789354890922));
#170853=CARTESIAN_POINT('Ctrl Pts',(17.9024394854094,-20.8988426003593,
1.36227065046302));
#170854=CARTESIAN_POINT('Ctrl Pts',(17.8353908192331,-20.8702039095181,
1.36665014265594));
#170855=CARTESIAN_POINT('Ctrl Pts',(17.7698814082307,-20.8381223644766,
1.37102963484885));
#170856=CARTESIAN_POINT('Ctrl Pts',(17.7062751622688,-20.8028027063711,
1.37540912704176));
#170857=CARTESIAN_POINT('Ctrl Pts',(17.6425561732691,-20.7674204436346,
1.37979638195116));
#170858=CARTESIAN_POINT('Ctrl Pts',(17.5807474952407,-20.7287888619662,
1.38418363686056));
#170859=CARTESIAN_POINT('Ctrl Pts',(17.5211845937122,-20.6871564166584,
1.38857089176995));
#170860=CARTESIAN_POINT('Ctrl Pts',(17.4806889445335,-20.6588513331858,
1.39155370038252));
#170861=CARTESIAN_POINT('Ctrl Pts',(17.4412307382319,-20.6291600265461,
1.39453650899508));
#170862=CARTESIAN_POINT('Ctrl Pts',(17.4029060715036,-20.5981706939196,
1.39751931760764));
#170863=CARTESIAN_POINT('Ctrl Pts',(17.3472596999084,-20.5531750275244,
1.40185027442008));
#170864=CARTESIAN_POINT('Ctrl Pts',(17.2937750955671,-20.5052554307103,
1.40618123123253));
#170865=CARTESIAN_POINT('Ctrl Pts',(17.2427818432682,-20.4546501286173,
1.41051218804497));
#170866=CARTESIAN_POINT('Ctrl Pts',(17.1918753395658,-20.4041309151483,
1.41483577712918));
#170867=CARTESIAN_POINT('Ctrl Pts',(17.1434521212288,-20.3509354147135,
1.41915936621338));
#170868=CARTESIAN_POINT('Ctrl Pts',(17.0978092707351,-20.2953424349241,
1.42348295529758));
#170869=CARTESIAN_POINT('Ctrl Pts',(17.0522098693201,-20.239802376101,1.42780242860111));
#170870=CARTESIAN_POINT('Ctrl Pts',(17.0093859027454,-20.1818697428219,
1.43212190190463));
#170871=CARTESIAN_POINT('Ctrl Pts',(16.9695971048709,-20.1218595743336,
1.43644137520815));
#170872=CARTESIAN_POINT('Ctrl Pts',(16.929832242749,-20.0618855061706,1.44075825004552));
#170873=CARTESIAN_POINT('Ctrl Pts',(16.8930992020878,-19.9998367937591,
1.44507512488289));
#170874=CARTESIAN_POINT('Ctrl Pts',(16.8596158068745,-19.9360593968666,
1.44939199972026));
#170875=CARTESIAN_POINT('Ctrl Pts',(16.8261408254926,-19.872298026194,1.45370778979737));
#170876=CARTESIAN_POINT('Ctrl Pts',(16.7959140985895,-19.8068092726922,
1.45802357987448));
#170877=CARTESIAN_POINT('Ctrl Pts',(16.7691077540283,-19.7399641246403,
1.46233936995159));
#170878=CARTESIAN_POINT('Ctrl Pts',(16.7422828062938,-19.6730725871276,
1.4666581551178));
#170879=CARTESIAN_POINT('Ctrl Pts',(16.7188831702512,-19.6048232350479,
1.470976940284));
#170880=CARTESIAN_POINT('Ctrl Pts',(16.6990325461928,-19.5356064272652,
1.47529572545021));
#170881=CARTESIAN_POINT('Ctrl Pts',(16.6791751535563,-19.4663660182415,
1.47961598321668));
#170882=CARTESIAN_POINT('Ctrl Pts',(16.6628692972426,-19.3961579800252,
1.48393624098314));
#170883=CARTESIAN_POINT('Ctrl Pts',(16.6501878709477,-19.325384534782,1.48825649874961));
#170884=CARTESIAN_POINT('Ctrl Pts',(16.6374866783545,-19.2545007763142,
1.49258349041979));
#170885=CARTESIAN_POINT('Ctrl Pts',(16.6284212611835,-19.1830503436799,
1.49691048208997));
#170886=CARTESIAN_POINT('Ctrl Pts',(16.6230126895585,-19.1114414474182,
1.50123747376015));
#170887=CARTESIAN_POINT('Ctrl Pts',(16.6189685454895,-19.0578974226401,
1.50447288948776));
#170888=CARTESIAN_POINT('Ctrl Pts',(16.6169678502335,-19.0042649285282,
1.50770830521537));
#170889=CARTESIAN_POINT('Ctrl Pts',(16.6170003908423,-18.9507135995066,
1.51094372094299));
#170890=CARTESIAN_POINT('Ctrl Pts',(16.7454193692601,-18.2258897638472,
0.53417740218321));
#170891=CARTESIAN_POINT('Ctrl Pts',(16.756562733977,-18.1953716990493,0.535943850225965));
#170892=CARTESIAN_POINT('Ctrl Pts',(16.7684073022959,-18.1651137736251,
0.537705175197931));
#170893=CARTESIAN_POINT('Ctrl Pts',(16.8090263232043,-18.0679964736271,
0.543420742649993));
#170894=CARTESIAN_POINT('Ctrl Pts',(16.8405517957402,-18.0023478894375,
0.547383536916499));
#170895=CARTESIAN_POINT('Ctrl Pts',(16.901832881024,-17.8899725787147,0.554496496727182));
#170896=CARTESIAN_POINT('Ctrl Pts',(16.9301570455683,-17.8425458373681,
0.55760883953424));
#170897=CARTESIAN_POINT('Ctrl Pts',(16.9790300312968,-17.7675396399683,
0.562757572939678));
#170898=CARTESIAN_POINT('Ctrl Pts',(16.9984537680169,-17.7392572348252,
0.56475409184634));
#170899=CARTESIAN_POINT('Ctrl Pts',(17.024861657968,-17.7027398407844,0.567411416226571));
#170900=CARTESIAN_POINT('Ctrl Pts',(17.0312343077344,-17.6940676455638,
0.568048528130771));
#170901=CARTESIAN_POINT('Ctrl Pts',(17.0417745351712,-17.6799508730185,
0.56909576351756));
#170902=CARTESIAN_POINT('Ctrl Pts',(17.0459029806939,-17.6744772186107,
0.56950434580879));
#170903=CARTESIAN_POINT('Ctrl Pts',(17.0539417418228,-17.6639261204056,
0.570296888065913));
#170904=CARTESIAN_POINT('Ctrl Pts',(17.0578486721602,-17.6588461828019,
0.570680710981603));
#170905=CARTESIAN_POINT('Ctrl Pts',(17.0669165480924,-17.6471659249275,
0.571568472289102));
#170906=CARTESIAN_POINT('Ctrl Pts',(17.0720937059783,-17.640578379844,0.572073056529223));
#170907=CARTESIAN_POINT('Ctrl Pts',(17.0861068749037,-17.6229639153252,
0.573432878399449));
#170908=CARTESIAN_POINT('Ctrl Pts',(17.0950142926235,-17.6119945888838,
0.574290992264062));
#170909=CARTESIAN_POINT('Ctrl Pts',(17.1997115915247,-17.4856674459239,
0.584307127752185));
#170910=CARTESIAN_POINT('Ctrl Pts',(17.3073680598168,-17.3807338434297,
0.593981628734713));
#170911=CARTESIAN_POINT('Ctrl Pts',(17.4998931155373,-17.229297183926,0.610137970609044));
#170912=CARTESIAN_POINT('Ctrl Pts',(17.57848060266,-17.1756272118375,0.616463122468588));
#170913=CARTESIAN_POINT('Ctrl Pts',(17.6992045390509,-17.1045927755265,
0.625584859652264));
#170914=CARTESIAN_POINT('Ctrl Pts',(17.7387200255397,-17.0830073848608,
0.628482638642888));
#170915=CARTESIAN_POINT('Ctrl Pts',(17.8009177282364,-17.0515644279514,
0.632877779770675));
#170916=CARTESIAN_POINT('Ctrl Pts',(17.8231334874371,-17.0408170653403,
0.634415901067499));
#170917=CARTESIAN_POINT('Ctrl Pts',(17.8514891312786,-17.0277062012849,
0.636334570305523));
#170918=CARTESIAN_POINT('Ctrl Pts',(17.8574579488358,-17.0249799968968,
0.636735978481852));
#170919=CARTESIAN_POINT('Ctrl Pts',(17.8665015249334,-17.0209001371136,
0.637340333513583));
#170920=CARTESIAN_POINT('Ctrl Pts',(17.8695669222081,-17.0195260055909,
0.637544521753834));
#170921=CARTESIAN_POINT('Ctrl Pts',(17.8758784976567,-17.0167147264572,
0.63796355787036));
#170922=CARTESIAN_POINT('Ctrl Pts',(17.8791249723721,-17.0152784686316,
0.638178343239903));
#170923=CARTESIAN_POINT('Ctrl Pts',(17.8864159254181,-17.0120748165946,
0.638659043199251));
#170924=CARTESIAN_POINT('Ctrl Pts',(17.8904623225654,-17.0103119024273,
0.638924681612913));
#170925=CARTESIAN_POINT('Ctrl Pts',(17.9007735920885,-17.005857856422,0.63959876083953));
#170926=CARTESIAN_POINT('Ctrl Pts',(17.9070460605558,-17.0031842891783,
0.640006155141074));
#170927=CARTESIAN_POINT('Ctrl Pts',(17.9427414388296,-16.9881729179746,
0.642310099755358));
#170928=CARTESIAN_POINT('Ctrl Pts',(17.9724290821328,-16.9764704755102,
0.644170672464985));
#170929=CARTESIAN_POINT('Ctrl Pts',(18.188544046162,-16.8968775790697,0.657394732564471));
#170930=CARTESIAN_POINT('Ctrl Pts',(18.3834474872641,-16.8548155383701,
0.667705158228814));
#170931=CARTESIAN_POINT('Ctrl Pts',(18.637122414328,-16.836479370595,0.681839177325682));
#170932=CARTESIAN_POINT('Ctrl Pts',(18.6930022077351,-16.8346593773269,
0.68498911271661));
#170933=CARTESIAN_POINT('Ctrl Pts',(18.7835696532868,-16.8352962233804,
0.690198379327331));
#170934=CARTESIAN_POINT('Ctrl Pts',(18.8182406796866,-16.8363924433602,
0.692217110253768));
#170935=CARTESIAN_POINT('Ctrl Pts',(18.8637193294802,-16.8389500656925,
0.694903409369141));
#170936=CARTESIAN_POINT('Ctrl Pts',(18.8745658967328,-16.83964388624,0.695546941582073));
#170937=CARTESIAN_POINT('Ctrl Pts',(18.8923113478785,-16.8409162879418,
0.696604644414029));
#170938=CARTESIAN_POINT('Ctrl Pts',(18.899213671785,-16.841445247549,0.697017255642141));
#170939=CARTESIAN_POINT('Ctrl Pts',(18.9125619584686,-16.8425340747035,
0.697817576326137));
#170940=CARTESIAN_POINT('Ctrl Pts',(18.9190082004218,-16.8430896587722,
0.698205147006114));
#170941=CARTESIAN_POINT('Ctrl Pts',(18.9338757417168,-16.8444397430067,
0.699101558928685));
#170942=CARTESIAN_POINT('Ctrl Pts',(18.942294986643,-16.8452551781747,0.699611052345321));
#170943=CARTESIAN_POINT('Ctrl Pts',(18.9649013266819,-16.8475815217057,
0.700984207427924));
#170944=CARTESIAN_POINT('Ctrl Pts',(18.9790782212912,-16.8491854089576,
0.701850773653737));
#170945=CARTESIAN_POINT('Ctrl Pts',(19.1068116688505,-16.8649456383207,
0.709708815719299));
#170946=CARTESIAN_POINT('Ctrl Pts',(19.2190442667893,-16.8881421586555,
0.716988267721187));
#170947=CARTESIAN_POINT('Ctrl Pts',(19.4859089498574,-16.9662739949165,
0.735128286995092));
#170948=CARTESIAN_POINT('Ctrl Pts',(19.6371119043171,-17.0303175560788,
0.746145432696012));
#170949=CARTESIAN_POINT('Ctrl Pts',(19.807930229791,-17.1273254183587,0.75862782643242));
#170950=CARTESIAN_POINT('Ctrl Pts',(19.8360557092467,-17.144173416957,0.760682322494398));
#170951=CARTESIAN_POINT('Ctrl Pts',(19.8699354611918,-17.1655530789304,
0.763145746535472));
#170952=CARTESIAN_POINT('Ctrl Pts',(19.8760707044643,-17.1694690792802,
0.763591376072764));
#170953=CARTESIAN_POINT('Ctrl Pts',(19.8856545194286,-17.1756560257318,
0.764286600623958));
#170954=CARTESIAN_POINT('Ctrl Pts',(19.8891167837211,-17.1779055088088,
0.764537575238687));
#170955=CARTESIAN_POINT('Ctrl Pts',(19.8955694038979,-17.1821247666374,
0.765004940135757));
#170956=CARTESIAN_POINT('Ctrl Pts',(19.8985613173316,-17.1840919819673,
0.765221489450688));
#170957=CARTESIAN_POINT('Ctrl Pts',(19.9053743893457,-17.1885964506168,
0.765714263610307));
#170958=CARTESIAN_POINT('Ctrl Pts',(19.9091922926673,-17.1911385306746,
0.765990160693723));
#170959=CARTESIAN_POINT('Ctrl Pts',(19.9208987306908,-17.198988077657,0.76683546444715));
#170960=CARTESIAN_POINT('Ctrl Pts',(19.928759921992,-17.2043363787021,0.7674021971589));
#170961=CARTESIAN_POINT('Ctrl Pts',(19.9989279786235,-17.2527694101189,
0.772455133012804));
#170962=CARTESIAN_POINT('Ctrl Pts',(20.0589236708848,-17.2991215283063,
0.776736064714976));
#170963=CARTESIAN_POINT('Ctrl Pts',(20.2235242540584,-17.4410253283913,
0.788766691494084));
#170964=CARTESIAN_POINT('Ctrl Pts',(20.3211978704125,-17.5439757776493,
0.796291212775601));
#170965=CARTESIAN_POINT('Ctrl Pts',(20.4457162138202,-17.7047877383316,
0.807543794352667));
#170966=CARTESIAN_POINT('Ctrl Pts',(20.481403118573,-17.7552994087573,0.811013082463597));
#170967=CARTESIAN_POINT('Ctrl Pts',(20.5349762828834,-17.8386438084752,
0.81669923004443));
#170968=CARTESIAN_POINT('Ctrl Pts',(20.554293322639,-17.8705151176844,0.818864946077263));
#170969=CARTESIAN_POINT('Ctrl Pts',(20.5782785347725,-17.91255314625,0.82171805014904));
#170970=CARTESIAN_POINT('Ctrl Pts',(20.5837221241766,-17.9222713310008,
0.822377370749431));
#170971=CARTESIAN_POINT('Ctrl Pts',(20.5924483618978,-17.9381423613318,
0.823453918609312));
#170972=CARTESIAN_POINT('Ctrl Pts',(20.5957777920247,-17.9442693431958,
0.823869468035583));
#170973=CARTESIAN_POINT('Ctrl Pts',(20.6021210313214,-17.9560812219315,
0.824670538111188));
#170974=CARTESIAN_POINT('Ctrl Pts',(20.6051393169819,-17.9617636366996,
0.825055893890783));
#170975=CARTESIAN_POINT('Ctrl Pts',(20.6119890785312,-17.9748025690981,
0.825940132333222));
#170976=CARTESIAN_POINT('Ctrl Pts',(20.6158033005595,-17.9821679872317,
0.826439617829988));
#170977=CARTESIAN_POINT('Ctrl Pts',(20.625817666256,-18.0017876427368,0.827770211341403));
#170978=CARTESIAN_POINT('Ctrl Pts',(20.6319419396316,-18.0140799681767,
0.828603961772518));
#170979=CARTESIAN_POINT('Ctrl Pts',(20.67748316056,-18.1077607295877,0.83495969875425));
#170980=CARTESIAN_POINT('Ctrl Pts',(20.7117633269927,-18.1915296052101,
0.840658553926819));
#170981=CARTESIAN_POINT('Ctrl Pts',(20.7851879883555,-18.4098724996177,
0.855533050089258));
#170982=CARTESIAN_POINT('Ctrl Pts',(20.8165299550453,-18.5466132606371,
0.864885055398191));
#170983=CARTESIAN_POINT('Ctrl Pts',(20.8410841531538,-18.740061165054,0.877655875524083));
#170984=CARTESIAN_POINT('Ctrl Pts',(20.845884637824,-18.7949464858018,0.881224623349047));
#170985=CARTESIAN_POINT('Ctrl Pts',(20.8499087278744,-18.8783362681687,
0.88650859906527));
#170986=CARTESIAN_POINT('Ctrl Pts',(20.8507068074099,-18.9067389214647,
0.88828401775567));
#170987=CARTESIAN_POINT('Ctrl Pts',(20.8509881596209,-18.9420875532205,
0.890456401079072));
#170988=CARTESIAN_POINT('Ctrl Pts',(20.8510092763639,-18.9490248623917,
0.890880955648094));
#170989=CARTESIAN_POINT('Ctrl Pts',(20.8509887258657,-18.9600047900095,
0.891549955799514));
#170990=CARTESIAN_POINT('Ctrl Pts',(20.8509695804609,-18.9640473292392,
0.891795630669776));
#170991=CARTESIAN_POINT('Ctrl Pts',(20.8509116364382,-18.9716710250809,
0.892257712671293));
#170992=CARTESIAN_POINT('Ctrl Pts',(20.8508753307681,-18.9752520943311,
0.892474250698219));
#170993=CARTESIAN_POINT('Ctrl Pts',(20.8507715424075,-18.9834398188553,
0.892968183478084));
#170994=CARTESIAN_POINT('Ctrl Pts',(20.8506981094313,-18.988046350801,0.893245242243488));
#170995=CARTESIAN_POINT('Ctrl Pts',(20.8504631736449,-19.000278450673,0.893978808018579));
#170996=CARTESIAN_POINT('Ctrl Pts',(20.8502754957042,-19.0079035280152,
0.894433888677758));
#170997=CARTESIAN_POINT('Ctrl Pts',(20.848670192472,-19.061374758166,0.897610771588053));
#170998=CARTESIAN_POINT('Ctrl Pts',(20.845804004915,-19.1071688816759,0.900257379866982));
#170999=CARTESIAN_POINT('Ctrl Pts',(20.8378738680996,-19.190382455053,0.904989165875819));
#171000=CARTESIAN_POINT('Ctrl Pts',(20.8332930167474,-19.2278269539272,
0.907089594987942));
#171001=CARTESIAN_POINT('Ctrl Pts',(20.8083554848241,-19.3945691353168,
0.916389495730702));
#171002=CARTESIAN_POINT('Ctrl Pts',(20.7770356154966,-19.5219342647907,
0.923366576445844));
#171003=CARTESIAN_POINT('Ctrl Pts',(20.7052127845892,-19.7290535564578,
0.935466841354512));
#171004=CARTESIAN_POINT('Ctrl Pts',(20.6710793550723,-19.8106111333967,
0.940438850852846));
#171005=CARTESIAN_POINT('Ctrl Pts',(20.6228630275673,-19.9081938682297,
0.946782330883236));
#171006=CARTESIAN_POINT('Ctrl Pts',(20.613504225402,-19.9264609143076,0.94798733709584));
#171007=CARTESIAN_POINT('Ctrl Pts',(20.5997291471433,-19.9524110069799,
0.949725671679413));
#171008=CARTESIAN_POINT('Ctrl Pts',(20.5955277532256,-19.9602072474063,
0.950251395298374));
#171009=CARTESIAN_POINT('Ctrl Pts',(20.5881609057574,-19.9736743667182,
0.951165660908251));
#171010=CARTESIAN_POINT('Ctrl Pts',(20.5850180256244,-19.9793575051611,
0.951553392582516));
#171011=CARTESIAN_POINT('Ctrl Pts',(20.578925774579,-19.9902551592022,0.952300605540826));
#171012=CARTESIAN_POINT('Ctrl Pts',(20.5759803176971,-19.9954717999949,
0.952659943299068));
#171013=CARTESIAN_POINT('Ctrl Pts',(20.5682083838618,-20.0091010696816,
0.953603141133994));
#171014=CARTESIAN_POINT('Ctrl Pts',(20.5633462080697,-20.0174930844778,
0.954188288616566));
#171015=CARTESIAN_POINT('Ctrl Pts',(20.5462827866204,-20.0464830949498,
0.956225129268232));
#171016=CARTESIAN_POINT('Ctrl Pts',(20.5337902835073,-20.0669067249354,
0.957687395725874));
#171017=CARTESIAN_POINT('Ctrl Pts',(20.4376925818721,-20.2181887111039,
0.968729193057548));
#171018=CARTESIAN_POINT('Ctrl Pts',(20.3402766470718,-20.3396818906598,
0.978844831797642));
#171019=CARTESIAN_POINT('Ctrl Pts',(20.1778923763589,-20.5019647485338,
0.994011770681932));
#171020=CARTESIAN_POINT('Ctrl Pts',(20.1225743791027,-20.5517117431381,
0.998935572874766));
#171021=CARTESIAN_POINT('Ctrl Pts',(20.028995869482,-20.6273472817382,1.00677231099476));
#171022=CARTESIAN_POINT('Ctrl Pts',(19.9923045149465,-20.6550775407114,
1.00973306955527));
#171023=CARTESIAN_POINT('Ctrl Pts',(19.9410807103848,-20.6912310236778,
1.01368767342682));
#171024=CARTESIAN_POINT('Ctrl Pts',(19.9273103005608,-20.7007077967887,
1.01473382801114));
#171025=CARTESIAN_POINT('Ctrl Pts',(19.9035320870702,-20.7166602283377,
1.01650952270634));
#171026=CARTESIAN_POINT('Ctrl Pts',(19.8935793755225,-20.7232161672246,
1.01724370883771));
#171027=CARTESIAN_POINT('Ctrl Pts',(19.8793553253973,-20.7324143869249,
1.0182795759814));
#171028=CARTESIAN_POINT('Ctrl Pts',(19.8751293410706,-20.7351259177989,
1.0185856686404));
#171029=CARTESIAN_POINT('Ctrl Pts',(19.8678307178282,-20.7397723813504,
1.01911139810944));
#171030=CARTESIAN_POINT('Ctrl Pts',(19.8647626892435,-20.7417144815897,
1.01933150798476));
#171031=CARTESIAN_POINT('Ctrl Pts',(19.8588028021837,-20.7454657207324,
1.01975735780632));
#171032=CARTESIAN_POINT('Ctrl Pts',(19.8559115711682,-20.7472757621329,
1.01996316072368));
#171033=CARTESIAN_POINT('Ctrl Pts',(19.8481018918748,-20.7521387406616,
1.02051699369924));
#171034=CARTESIAN_POINT('Ctrl Pts',(19.843175233503,-20.7551785308962,1.02086416262428));
#171035=CARTESIAN_POINT('Ctrl Pts',(19.8248594182825,-20.7663760757551,
1.02214689117409));
#171036=CARTESIAN_POINT('Ctrl Pts',(19.811391855142,-20.774405453696,1.02307441286469));
#171037=CARTESIAN_POINT('Ctrl Pts',(19.6817561764723,-20.8497549800986,
1.03186595120302));
#171038=CARTESIAN_POINT('Ctrl Pts',(19.5595042888919,-20.9060389756439,
1.03912865015386));
#171039=CARTESIAN_POINT('Ctrl Pts',(19.2810393565962,-21.0034044001591,
1.05514839286962));
#171040=CARTESIAN_POINT('Ctrl Pts',(19.1238252041838,-21.0389931039599,
1.06389558320799));
#171041=CARTESIAN_POINT('Ctrl Pts',(18.9455568207444,-21.0584854458993,
1.07436835008178));
#171042=CARTESIAN_POINT('Ctrl Pts',(18.9269811212476,-21.0602683595867,
1.07546547260087));
#171043=CARTESIAN_POINT('Ctrl Pts',(18.899884412029,-21.0625080218997,1.07707529684192));
#171044=CARTESIAN_POINT('Ctrl Pts',(18.8913800445507,-21.0631592235043,
1.07758189314329));
#171045=CARTESIAN_POINT('Ctrl Pts',(18.8764405208529,-21.0642124108122,
1.07847428179421));
#171046=CARTESIAN_POINT('Ctrl Pts',(18.8700069918926,-21.0646364256793,
1.07885937747679));
#171047=CARTESIAN_POINT('Ctrl Pts',(18.8574944176068,-21.06540370039,1.07960994174849));
#171048=CARTESIAN_POINT('Ctrl Pts',(18.8514156251003,-21.0657501370267,
1.07997530663645));
#171049=CARTESIAN_POINT('Ctrl Pts',(18.8368538202104,-21.066517020409,1.08085232479858));
#171050=CARTESIAN_POINT('Ctrl Pts',(18.8283696560654,-21.0669126465785,
1.08136475180461));
#171051=CARTESIAN_POINT('Ctrl Pts',(18.7975852189731,-21.0681625528504,
1.08322945501518));
#171052=CARTESIAN_POINT('Ctrl Pts',(18.7752747833154,-21.0687152294586,
1.08459112605128));
#171053=CARTESIAN_POINT('Ctrl Pts',(18.5696370501106,-21.0705570509026,
1.09724050441705));
#171054=CARTESIAN_POINT('Ctrl Pts',(18.3869095213298,-21.0483780083643,
1.10930507026757));
#171055=CARTESIAN_POINT('Ctrl Pts',(18.1303766037215,-20.9827574163749,
1.12678910466413));
#171056=CARTESIAN_POINT('Ctrl Pts',(18.0526132115985,-20.9580036617207,
1.13214925943526));
#171057=CARTESIAN_POINT('Ctrl Pts',(17.9424743182601,-20.9157976743825,
1.13967023168194));
#171058=CARTESIAN_POINT('Ctrl Pts',(17.9088205239887,-20.901895743746,1.14195787695923));
#171059=CARTESIAN_POINT('Ctrl Pts',(17.868691505981,-20.8840937708203,1.14465883255332));
#171060=CARTESIAN_POINT('Ctrl Pts',(17.8618592503056,-20.8810193481767,
1.14511773346991));
#171061=CARTESIAN_POINT('Ctrl Pts',(17.8512529429529,-20.8761787840294,
1.14582846849455));
#171062=CARTESIAN_POINT('Ctrl Pts',(17.8474676197023,-20.874437697042,1.1460817951661));
#171063=CARTESIAN_POINT('Ctrl Pts',(17.8404514818725,-20.8711854436266,
1.14655069120322));
#171064=CARTESIAN_POINT('Ctrl Pts',(17.8372193748333,-20.8696773012933,
1.14676643650128));
#171065=CARTESIAN_POINT('Ctrl Pts',(17.829913226265,-20.8662456483881,1.14725355039617));
#171066=CARTESIAN_POINT('Ctrl Pts',(17.8258415152605,-20.8643173021946,
1.14752461591591));
#171067=CARTESIAN_POINT('Ctrl Pts',(17.8135518609585,-20.8584488665955,
1.14834164637307));
#171068=CARTESIAN_POINT('Ctrl Pts',(17.8053530516742,-20.8544686356715,
1.14888518455738));
#171069=CARTESIAN_POINT('Ctrl Pts',(17.742406533295,-20.823406450517,1.15304834161828));
#171070=CARTESIAN_POINT('Ctrl Pts',(17.6888228907673,-20.794016825117,1.15653478817146));
#171071=CARTESIAN_POINT('Ctrl Pts',(17.4971417817146,-20.6778211700197,
1.16906404356491));
#171072=CARTESIAN_POINT('Ctrl Pts',(17.3679313976352,-20.5774658581177,
1.17766507019037));
#171073=CARTESIAN_POINT('Ctrl Pts',(17.1948923637841,-20.4077225768788,
1.191113614336));
#171074=CARTESIAN_POINT('Ctrl Pts',(17.1414403955231,-20.3490441937331,
1.19560092452114));
#171075=CARTESIAN_POINT('Ctrl Pts',(17.0791845743373,-20.2724735680201,
1.2013595674809));
#171076=CARTESIAN_POINT('Ctrl Pts',(17.0671668213682,-20.2572707207976,
1.20249829610772));
#171077=CARTESIAN_POINT('Ctrl Pts',(17.050084020611,-20.2350397285934,1.20415785262012));
#171078=CARTESIAN_POINT('Ctrl Pts',(17.0448505163626,-20.2281418374624,
1.20467201801049));
#171079=CARTESIAN_POINT('Ctrl Pts',(17.0357829816299,-20.2160370908401,
1.20557306108346));
#171080=CARTESIAN_POINT('Ctrl Pts',(17.0319301924208,-20.2108443816442,
1.2059591978554));
#171081=CARTESIAN_POINT('Ctrl Pts',(17.0245195218137,-20.2007602167472,
1.20670834888397));
#171082=CARTESIAN_POINT('Ctrl Pts',(17.0209586919641,-20.1958709981395,
1.20707124330529));
#171083=CARTESIAN_POINT('Ctrl Pts',(17.0125345191679,-20.1841993553616,
1.20793681684641));
#171084=CARTESIAN_POINT('Ctrl Pts',(17.0076902625268,-20.177403337777,1.20844022578092));
#171085=CARTESIAN_POINT('Ctrl Pts',(16.9905656874668,-20.1530761607897,
1.21024028032476));
#171086=CARTESIAN_POINT('Ctrl Pts',(16.9785115316578,-20.1353880728047,
1.21154550124966));
#171087=CARTESIAN_POINT('Ctrl Pts',(16.8609883990679,-19.9571884619835,
1.22466377252393));
#171088=CARTESIAN_POINT('Ctrl Pts',(16.7775784213282,-19.7832402364215,
1.23734170066882));
#171089=CARTESIAN_POINT('Ctrl Pts',(16.6954799616009,-19.5281125874455,
1.25502391781768));
#171090=CARTESIAN_POINT('Ctrl Pts',(16.6761041766622,-19.4545296219884,
1.26000955504588));
#171091=CARTESIAN_POINT('Ctrl Pts',(16.6536719489235,-19.3458808933151,
1.26707452376771));
#171092=CARTESIAN_POINT('Ctrl Pts',(16.6474610384553,-19.3115308720113,
1.26926547983072));
#171093=CARTESIAN_POINT('Ctrl Pts',(16.6409663500992,-19.2697323453033,
1.27186750610064));
#171094=CARTESIAN_POINT('Ctrl Pts',(16.639869047353,-19.2624178792355,1.27232047861227));
#171095=CARTESIAN_POINT('Ctrl Pts',(16.6382167990403,-19.2509965648377,
1.27302393473657));
#171096=CARTESIAN_POINT('Ctrl Pts',(16.6376355523249,-19.2468936662818,
1.27327586526393));
#171097=CARTESIAN_POINT('Ctrl Pts',(16.6365763775123,-19.2392557606341,
1.2737433840514));
#171098=CARTESIAN_POINT('Ctrl Pts',(16.6360953416556,-19.2357212874404,
1.2739591405538));
#171099=CARTESIAN_POINT('Ctrl Pts',(16.6350235911957,-19.2276946907583,
1.27444778780642));
#171100=CARTESIAN_POINT('Ctrl Pts',(16.6344383637596,-19.2232018874071,
1.27472036628636));
#171101=CARTESIAN_POINT('Ctrl Pts',(16.6327408137607,-19.2098348694521,
1.27552865093633));
#171102=CARTESIAN_POINT('Ctrl Pts',(16.6316702820028,-19.200955319001,1.27606205837468));
#171103=CARTESIAN_POINT('Ctrl Pts',(16.6239226733556,-19.1330753311044,
1.28011460693802));
#171104=CARTESIAN_POINT('Ctrl Pts',(16.6196735818517,-19.0738185473203,
1.28350784889789));
#171105=CARTESIAN_POINT('Ctrl Pts',(16.6173229666981,-18.9941773248179,
1.28796711722882));
#171106=CARTESIAN_POINT('Ctrl Pts',(16.6170159594122,-18.9738905047956,
1.28909419685705));
#171107=CARTESIAN_POINT('Ctrl Pts',(16.6168948152901,-18.813805207517,1.2979391220944));
#171108=CARTESIAN_POINT('Ctrl Pts',(16.6306361033606,-18.674341220692,1.30537418636845));
#171109=CARTESIAN_POINT('Ctrl Pts',(16.6757502479721,-18.4485303115064,
1.31812043025327));
#171110=CARTESIAN_POINT('Ctrl Pts',(16.6991412232676,-18.3610510614871,
1.32323611835779));
#171111=CARTESIAN_POINT('Ctrl Pts',(16.7324404237939,-18.2623358209319,
1.3293438777088));
#171112=CARTESIAN_POINT('Ctrl Pts',(16.7369541499677,-18.2493725904713,
1.33015264909307));
#171113=CARTESIAN_POINT('Ctrl Pts',(16.7428594802954,-18.2329294480821,
1.33118740041875));
#171114=CARTESIAN_POINT('Ctrl Pts',(16.7441347600493,-18.2294078921804,
1.33140952898772));
#171115=CARTESIAN_POINT('Ctrl Pts',(16.7454193692336,-18.2258897639197,
1.33163196665472));
#171116=CARTESIAN_POINT('Origin',(18.734,-18.952,0.));
#171117=CARTESIAN_POINT('',(16.7454193691877,-18.2258897640454,2.35747631421306));
#171118=CARTESIAN_POINT('',(16.7452305870807,-18.2258208582162,2.13351566426921));
#171119=CARTESIAN_POINT('',(16.7454193692319,-18.2258897639242,0.));
#171120=CARTESIAN_POINT('Ctrl Pts',(16.7454193691877,-18.2258897640453,
2.35747631421306));
#171121=CARTESIAN_POINT('Ctrl Pts',(16.742191647268,-18.2347294483981,2.35692305832686));
#171122=CARTESIAN_POINT('Ctrl Pts',(16.7390229051106,-18.2435905499536,
2.35636788652136));
#171123=CARTESIAN_POINT('Ctrl Pts',(16.7330803313949,-18.2605645458309,
2.35530317645736));
#171124=CARTESIAN_POINT('Ctrl Pts',(16.7302965273719,-18.2686736519259,
2.35479398625594));
#171125=CARTESIAN_POINT('Ctrl Pts',(16.7255041834798,-18.2829146638836,
2.35389872613313));
#171126=CARTESIAN_POINT('Ctrl Pts',(16.7234742637549,-18.2890392964446,
2.35351336858945));
#171127=CARTESIAN_POINT('Ctrl Pts',(16.7195884540897,-18.300945475638,2.35276355646451));
#171128=CARTESIAN_POINT('Ctrl Pts',(16.7177293753157,-18.3067259211549,
2.35239921146551));
#171129=CARTESIAN_POINT('Ctrl Pts',(16.7133468272281,-18.3205564735102,
2.35152668444952));
#171130=CARTESIAN_POINT('Ctrl Pts',(16.7108465738788,-18.3286137770769,
2.3510177453064));
#171131=CARTESIAN_POINT('Ctrl Pts',(16.7020108004384,-18.3577010113374,
2.34917806413336));
#171132=CARTESIAN_POINT('Ctrl Pts',(16.6959546544632,-18.3788137235067,
2.3478382462076));
#171133=CARTESIAN_POINT('Ctrl Pts',(16.641457713344,-18.58059376658,2.33498642094185));
#171134=CARTESIAN_POINT('Ctrl Pts',(16.616843652966,-18.7668066908484,2.32266065705822));
#171135=CARTESIAN_POINT('Ctrl Pts',(16.6170536898947,-19.016790561049,2.30615864857607));
#171136=CARTESIAN_POINT('Ctrl Pts',(16.6199199087135,-19.0797716781136,
2.30201615293556));
#171137=CARTESIAN_POINT('Ctrl Pts',(16.6300811392499,-19.1922138793031,
2.29473640421839));
#171138=CARTESIAN_POINT('Ctrl Pts',(16.6363255949835,-19.2417244169326,
2.29157204903625));
#171139=CARTESIAN_POINT('Ctrl Pts',(16.6455655230035,-19.2986864772174,
2.28801329944128));
#171140=CARTESIAN_POINT('Ctrl Pts',(16.6468596252838,-19.3063940444386,
2.28753351543509));
#171141=CARTESIAN_POINT('Ctrl Pts',(16.6489941838878,-19.3186899263177,
2.28677110884327));
#171142=CARTESIAN_POINT('Ctrl Pts',(16.6498071584404,-19.3232828509857,
2.28648699258429));
#171143=CARTESIAN_POINT('Ctrl Pts',(16.6512728103301,-19.3314065698001,
2.28598569190362));
#171144=CARTESIAN_POINT('Ctrl Pts',(16.6519192987852,-19.3349384365235,
2.2857681597343));
#171145=CARTESIAN_POINT('Ctrl Pts',(16.6533073569515,-19.3424141755541,
2.28530860903462));
#171146=CARTESIAN_POINT('Ctrl Pts',(16.6540511539905,-19.3463575812757,
2.28506671893067));
#171147=CARTESIAN_POINT('Ctrl Pts',(16.6560859637875,-19.3569796646717,
2.28441650041225));
#171148=CARTESIAN_POINT('Ctrl Pts',(16.6573979731469,-19.3636543399822,
2.28400935192934));
#171149=CARTESIAN_POINT('Ctrl Pts',(16.6640292710389,-19.3965515595136,
2.28200921964718));
#171150=CARTESIAN_POINT('Ctrl Pts',(16.6698134504046,-19.4226792400825,
2.28044127498456));
#171151=CARTESIAN_POINT('Ctrl Pts',(16.6879077713527,-19.4976482032919,
2.27598365064359));
#171152=CARTESIAN_POINT('Ctrl Pts',(16.7014678574174,-19.5461709650004,
2.27314936331566));
#171153=CARTESIAN_POINT('Ctrl Pts',(16.7568102839577,-19.7200193903671,
2.2630318424694));
#171154=CARTESIAN_POINT('Ctrl Pts',(16.8085639996897,-19.8418492049444,
2.25599589812605));
#171155=CARTESIAN_POINT('Ctrl Pts',(16.9207548644365,-20.0495633359862,
2.24300920133381));
#171156=CARTESIAN_POINT('Ctrl Pts',(16.9768431251024,-20.1372842985294,
2.23716708890243));
#171157=CARTESIAN_POINT('Ctrl Pts',(17.0475681398124,-20.2317789787875,
2.23025034436802));
#171158=CARTESIAN_POINT('Ctrl Pts',(17.0561041215743,-20.2429500612168,
2.2294222526471));
#171159=CARTESIAN_POINT('Ctrl Pts',(17.0699092574628,-20.2606486739674,
2.22809314038657));
#171160=CARTESIAN_POINT('Ctrl Pts',(17.0751071295488,-20.2672314596875,
2.22759494147258));
#171161=CARTESIAN_POINT('Ctrl Pts',(17.0843685933005,-20.278818289363,2.22671109752194));
#171162=CARTESIAN_POINT('Ctrl Pts',(17.0884162008142,-20.283835015832,2.2263260965131));
#171163=CARTESIAN_POINT('Ctrl Pts',(17.0968603459561,-20.2942036825246,
2.22552548768125));
#171164=CARTESIAN_POINT('Ctrl Pts',(17.1012603578281,-20.2995526822103,
2.22510974180079));
#171165=CARTESIAN_POINT('Ctrl Pts',(17.1126754486993,-20.3132917775771,
2.22403476649502));
#171166=CARTESIAN_POINT('Ctrl Pts',(17.1197293707355,-20.3216492006401,
2.22337395481139));
#171167=CARTESIAN_POINT('Ctrl Pts',(17.1499117473638,-20.3568519484336,
2.22056071772465));
#171168=CARTESIAN_POINT('Ctrl Pts',(17.173646434622,-20.3831677406774,2.21838328353239));
#171169=CARTESIAN_POINT('Ctrl Pts',(17.2376865338461,-20.4506846956561,
2.2125935663988));
#171170=CARTESIAN_POINT('Ctrl Pts',(17.2790313529665,-20.4908551302041,
2.20893872119819));
#171171=CARTESIAN_POINT('Ctrl Pts',(17.4217681512704,-20.6186378809442,
2.19659998968109));
#171172=CARTESIAN_POINT('Ctrl Pts',(17.5298270513337,-20.6983094339051,
2.18767358335912));
#171173=CARTESIAN_POINT('Ctrl Pts',(17.7216270867672,-20.8134091984661,
2.17297278913589));
#171174=CARTESIAN_POINT('Ctrl Pts',(17.8014472693961,-20.8546540122369,
2.16715226193123));
#171175=CARTESIAN_POINT('Ctrl Pts',(17.892492001079,-20.894587563985,2.16101026085349));
#171176=CARTESIAN_POINT('Ctrl Pts',(17.9013574906196,-20.8984040216945,
2.16041725927675));
#171177=CARTESIAN_POINT('Ctrl Pts',(17.914496659348,-20.9039540304203,2.15954621082074));
#171178=CARTESIAN_POINT('Ctrl Pts',(17.9187502541619,-20.9057344023827,
2.15926542624076));
#171179=CARTESIAN_POINT('Ctrl Pts',(17.9263117558392,-20.9088703276771,
2.15876846066808));
#171180=CARTESIAN_POINT('Ctrl Pts',(17.9296173089669,-20.9102314128161,
2.1585519476452));
#171181=CARTESIAN_POINT('Ctrl Pts',(17.9367125522005,-20.9131319324304,
2.15808880166515));
#171182=CARTESIAN_POINT('Ctrl Pts',(17.9405032501498,-20.9146687543866,
2.15784232687763));
#171183=CARTESIAN_POINT('Ctrl Pts',(17.9509339896548,-20.918862418058,2.1571666973332));
#171184=CARTESIAN_POINT('Ctrl Pts',(17.9575831481224,-20.921496642183,2.15673888599771));
#171185=CARTESIAN_POINT('Ctrl Pts',(17.993357975345,-20.9354603706962,2.15445185884578));
#171186=CARTESIAN_POINT('Ctrl Pts',(18.0227201246813,-20.9461782326752,
2.15262711556594));
#171187=CARTESIAN_POINT('Ctrl Pts',(18.2073709256909,-21.008982258067,2.14141263178207));
#171188=CARTESIAN_POINT('Ctrl Pts',(18.3680442167472,-21.0435551359027,
2.13275774562994));
#171189=CARTESIAN_POINT('Ctrl Pts',(18.6477495766403,-21.0704853923423,
2.1173762373682));
#171190=CARTESIAN_POINT('Ctrl Pts',(18.7651027779518,-21.0720110415517,
2.11083587710707));
#171191=CARTESIAN_POINT('Ctrl Pts',(18.8962303130863,-21.062823217679,2.10313519787881));
#171192=CARTESIAN_POINT('Ctrl Pts',(18.9104790297499,-21.0616797074229,
2.10229342675773));
#171193=CARTESIAN_POINT('Ctrl Pts',(18.9331364557481,-21.0596302275954,
2.1009465044696));
#171194=CARTESIAN_POINT('Ctrl Pts',(18.9415533581131,-21.0588180046348,
2.10044429687156));
#171195=CARTESIAN_POINT('Ctrl Pts',(18.9563884338819,-21.0572966721817,
2.09955579480158));
#171196=CARTESIAN_POINT('Ctrl Pts',(18.9628086882494,-21.056608580278,2.09917016678875));
#171197=CARTESIAN_POINT('Ctrl Pts',(18.9760805752753,-21.0551247163706,
2.09837067025549));
#171198=CARTESIAN_POINT('Ctrl Pts',(18.9829316599811,-21.054324809453,2.09795667559764));
#171199=CARTESIAN_POINT('Ctrl Pts',(19.0005060015871,-21.0521857850952,
2.09689134106119));
#171200=CARTESIAN_POINT('Ctrl Pts',(19.0112230382498,-21.0507980277006,
2.0962384726535));
#171201=CARTESIAN_POINT('Ctrl Pts',(19.0558971022456,-21.0446650103507,
2.09350326012465));
#171202=CARTESIAN_POINT('Ctrl Pts',(19.0897453953052,-21.0391774212423,
2.09139760274706));
#171203=CARTESIAN_POINT('Ctrl Pts',(19.1775689127627,-21.0227408659694,
2.0858439983357));
#171204=CARTESIAN_POINT('Ctrl Pts',(19.2312739323303,-21.0105040518219,
2.08235768089844));
#171205=CARTESIAN_POINT('Ctrl Pts',(19.3900380388603,-20.9677537327037,
2.07178961959005));
#171206=CARTESIAN_POINT('Ctrl Pts',(19.4932692369694,-20.931180582558,2.06455947997301));
#171207=CARTESIAN_POINT('Ctrl Pts',(19.6343931269209,-20.8685104449588,
2.05435928051722));
#171208=CARTESIAN_POINT('Ctrl Pts',(19.6749881689147,-20.8489084100359,
2.05138765429304));
#171209=CARTESIAN_POINT('Ctrl Pts',(19.7364760283702,-20.8167579220294,
2.04685421020773));
#171210=CARTESIAN_POINT('Ctrl Pts',(19.7578295402099,-20.8051199182004,
2.04527366739353));
#171211=CARTESIAN_POINT('Ctrl Pts',(19.791519323121,-20.7859983160153,2.04277500044323));
#171212=CARTESIAN_POINT('Ctrl Pts',(19.8039875121088,-20.7787522227219,
2.04184916003008));
#171213=CARTESIAN_POINT('Ctrl Pts',(19.8483459158365,-20.7523626212031,
2.03855370498121));
#171214=CARTESIAN_POINT('Ctrl Pts',(19.879806499127,-20.732505614515,2.03621344760067));
#171215=CARTESIAN_POINT('Ctrl Pts',(19.9166872116085,-20.7078449027583,
2.03348122807795));
#171216=CARTESIAN_POINT('Ctrl Pts',(19.9226246903646,-20.7038309598396,
2.03304172238286));
#171217=CARTESIAN_POINT('Ctrl Pts',(19.9322733931313,-20.6972364610481,
2.03232824099036));
#171218=CARTESIAN_POINT('Ctrl Pts',(19.93599688225,-20.6946740732551,2.03205308500801));
#171219=CARTESIAN_POINT('Ctrl Pts',(19.9426437500345,-20.6900684698074,
2.03156226478174));
#171220=CARTESIAN_POINT('Ctrl Pts',(19.945570188268,-20.6880297807783,2.03134629975521));
#171221=CARTESIAN_POINT('Ctrl Pts',(19.9518925993929,-20.6836015298445,
2.03088000667716));
#171222=CARTESIAN_POINT('Ctrl Pts',(19.9552866875967,-20.6812093769105,
2.03062985969465));
#171223=CARTESIAN_POINT('Ctrl Pts',(19.9647377843521,-20.6745065383444,
2.0299337298816));
#171224=CARTESIAN_POINT('Ctrl Pts',(19.9707792256063,-20.670173861779,2.02948922907074));
#171225=CARTESIAN_POINT('Ctrl Pts',(20.0055417194514,-20.6449652521705,
2.02693360519926));
#171226=CARTESIAN_POINT('Ctrl Pts',(20.033758608939,-20.6233998870952,2.02486724857726));
#171227=CARTESIAN_POINT('Ctrl Pts',(20.1223549709297,-20.5520868550003,
2.01835813036604));
#171228=CARTESIAN_POINT('Ctrl Pts',(20.1805283151879,-20.4996967420553,
2.01405024523169));
#171229=CARTESIAN_POINT('Ctrl Pts',(20.3685617440419,-20.3104701293267,
1.99949831309707));
#171230=CARTESIAN_POINT('Ctrl Pts',(20.4829781411939,-20.1596021362546,
1.98942970458877));
#171231=CARTESIAN_POINT('Ctrl Pts',(20.5866552886593,-19.9766134412949,
1.97719372375848));
#171232=CARTESIAN_POINT('Ctrl Pts',(20.5971086305613,-19.9574802341664,
1.9759154173762));
#171233=CARTESIAN_POINT('Ctrl Pts',(20.6111823235174,-19.9307472919201,
1.97412940224031));
#171234=CARTESIAN_POINT('Ctrl Pts',(20.6150558848979,-19.9232818807924,
1.97363064816277));
#171235=CARTESIAN_POINT('Ctrl Pts',(20.6216461219928,-19.9103933982634,
1.97276951079539));
#171236=CARTESIAN_POINT('Ctrl Pts',(20.6243841851611,-19.904981331939,1.97240788381888));
#171237=CARTESIAN_POINT('Ctrl Pts',(20.6299885961669,-19.8937844355218,
1.97165964076125));
#171238=CARTESIAN_POINT('Ctrl Pts',(20.6328518121593,-19.8879981163514,
1.97127291990969));
#171239=CARTESIAN_POINT('Ctrl Pts',(20.6394660743292,-19.8744759900004,
1.97036903943696));
#171240=CARTESIAN_POINT('Ctrl Pts',(20.64319653363,-19.8667302909141,1.9698511696023));
#171241=CARTESIAN_POINT('Ctrl Pts',(20.6550374899063,-19.8417564549656,
1.96818096005817));
#171242=CARTESIAN_POINT('Ctrl Pts',(20.6629625844605,-19.8244419163164,
1.96702224650926));
#171243=CARTESIAN_POINT('Ctrl Pts',(20.7016633657586,-19.7367835081093,
1.96115072129043));
#171244=CARTESIAN_POINT('Ctrl Pts',(20.7288263091356,-19.6649165310286,
1.95631684499926));
#171245=CARTESIAN_POINT('Ctrl Pts',(20.7859350761981,-19.484770034785,1.94416142901015));
#171246=CARTESIAN_POINT('Ctrl Pts',(20.811284678941,-19.3752803138305,1.93673372124309));
#171247=CARTESIAN_POINT('Ctrl Pts',(20.8387416783276,-19.1911976000624,
1.92444377814641));
#171248=CARTESIAN_POINT('Ctrl Pts',(20.8458104712599,-19.1175620615204,
1.91958263215513));
#171249=CARTESIAN_POINT('Ctrl Pts',(20.8508466541166,-19.0014102367269,
1.91212805660246));
#171250=CARTESIAN_POINT('Ctrl Pts',(20.8514115646084,-18.9590675444051,
1.90945536089138));
#171251=CARTESIAN_POINT('Ctrl Pts',(20.8505820385815,-18.9092793911404,
1.90638686384221));
#171252=CARTESIAN_POINT('Ctrl Pts',(20.8504184733629,-18.9018260442319,
1.90592946551947));
#171253=CARTESIAN_POINT('Ctrl Pts',(20.8500901260508,-18.889768140469,1.90519283369693));
#171254=CARTESIAN_POINT('Ctrl Pts',(20.8499496804811,-18.8851630602953,
1.90491229223299));
#171255=CARTESIAN_POINT('Ctrl Pts',(20.8496735777288,-18.8769860764492,
1.90441559481882));
#171256=CARTESIAN_POINT('Ctrl Pts',(20.8495439067984,-18.8734140260176,
1.90419910818447));
#171257=CARTESIAN_POINT('Ctrl Pts',(20.8492463489532,-18.8657524806071,
1.90373583898263));
#171258=CARTESIAN_POINT('Ctrl Pts',(20.8490756501035,-18.8616631506368,
1.90348921552593));
#171259=CARTESIAN_POINT('Ctrl Pts',(20.8485735874786,-18.850418237488,1.90281275807648));
#171260=CARTESIAN_POINT('Ctrl Pts',(20.8482177600928,-18.8432637246195,
1.9023842729894));
#171261=CARTESIAN_POINT('Ctrl Pts',(20.8461060910646,-18.8047466814009,
1.90008709494134));
#171262=CARTESIAN_POINT('Ctrl Pts',(20.8436886072698,-18.7734225730965,
1.89825323777532));
#171263=CARTESIAN_POINT('Ctrl Pts',(20.8243542322785,-18.5793237258596,
1.88703960378519));
#171264=CARTESIAN_POINT('Ctrl Pts',(20.7893060586996,-18.4188980447585,
1.87839183547954));
#171265=CARTESIAN_POINT('Ctrl Pts',(20.6980565429817,-18.1533186682206,
1.86302000638181));
#171266=CARTESIAN_POINT('Ctrl Pts',(20.6508708197679,-18.0459034576789,
1.85648178334411));
#171267=CARTESIAN_POINT('Ctrl Pts',(20.5882363068399,-17.9303831276721,
1.84878351034564));
#171268=CARTESIAN_POINT('Ctrl Pts',(20.5812962745788,-17.9178869624485,
1.84794177047477));
#171269=CARTESIAN_POINT('Ctrl Pts',(20.5700502057172,-17.8981118922739,
1.84659488931344));
#171270=CARTESIAN_POINT('Ctrl Pts',(20.5658261032948,-17.8907867200022,
1.84609269131902));
#171271=CARTESIAN_POINT('Ctrl Pts',(20.5582992308094,-17.8779129414109,
1.84520420099984));
#171272=CARTESIAN_POINT('Ctrl Pts',(20.5550147293013,-17.8723537397822,
1.84481857508423));
#171273=CARTESIAN_POINT('Ctrl Pts',(20.548169063422,-17.8608871792916,1.84401907775769));
#171274=CARTESIAN_POINT('Ctrl Pts',(20.544604361378,-17.854982031597,1.84360508018427));
#171275=CARTESIAN_POINT('Ctrl Pts',(20.5353808316011,-17.8398701128789,
1.84253972732813));
#171276=CARTESIAN_POINT('Ctrl Pts',(20.5296803011461,-17.8306891440899,
1.84188684340652));
#171277=CARTESIAN_POINT('Ctrl Pts',(20.5055998716988,-17.7925610653245,
1.839151474149));
#171278=CARTESIAN_POINT('Ctrl Pts',(20.4865891858849,-17.7640203376469,
1.83704567214399));
#171279=CARTESIAN_POINT('Ctrl Pts',(20.4352615146701,-17.6908771120922,
1.83149159397724));
#171280=CARTESIAN_POINT('Ctrl Pts',(20.4018838923408,-17.6470539543977,
1.82800493913055));
#171281=CARTESIAN_POINT('Ctrl Pts',(20.2972294796716,-17.5202306284797,
1.81743623275423));
#171282=CARTESIAN_POINT('Ctrl Pts',(20.2211934822354,-17.4414034227911,
1.81020578731047));
#171283=CARTESIAN_POINT('Ctrl Pts',(20.0508008596991,-17.2901440020614,
1.79515491381617));
#171284=CARTESIAN_POINT('Ctrl Pts',(19.9557263873125,-17.2190484618821,
1.787362537917));
#171285=CARTESIAN_POINT('Ctrl Pts',(19.8471142469255,-17.1512345095083,
1.77945379048602));
#171286=CARTESIAN_POINT('Ctrl Pts',(19.8390027594011,-17.146245701111,1.77886882479014));
#171287=CARTESIAN_POINT('Ctrl Pts',(19.8269353937759,-17.1389356726576,
1.77800728659057));
#171288=CARTESIAN_POINT('Ctrl Pts',(19.8230053212772,-17.1365723806239,
1.7777280602783));
#171289=CARTESIAN_POINT('Ctrl Pts',(19.8160002025276,-17.1323908873519,
1.77723281004933));
#171290=CARTESIAN_POINT('Ctrl Pts',(19.8129282087537,-17.1305676839048,
1.77701646273488));
#171291=CARTESIAN_POINT('Ctrl Pts',(19.8063147171267,-17.1266652328655,
1.77655250918701));
#171292=CARTESIAN_POINT('Ctrl Pts',(19.8027717902178,-17.124588517665,1.77630506722681));
#171293=CARTESIAN_POINT('Ctrl Pts',(19.7929782376184,-17.1188861718591,
1.77562405119693));
#171294=CARTESIAN_POINT('Ctrl Pts',(19.7867149897119,-17.1152821750386,
1.77519185638822));
#171295=CARTESIAN_POINT('Ctrl Pts',(19.7523472612142,-17.0957398524043,
1.77283781471752));
#171296=CARTESIAN_POINT('Ctrl Pts',(19.7238975418857,-17.080413508965,1.77095287569351));
#171297=CARTESIAN_POINT('Ctrl Pts',(19.5499866865743,-16.9918005114291,
1.75974323446217));
#171298=CARTESIAN_POINT('Ctrl Pts',(19.3968036625889,-16.9348436998903,
1.75113480058229));
#171299=CARTESIAN_POINT('Ctrl Pts',(19.1250576175935,-16.8681504438336,
1.73581694083408));
#171300=CARTESIAN_POINT('Ctrl Pts',(19.0094274171547,-16.8497418085637,
1.7292910629989));
#171301=CARTESIAN_POINT('Ctrl Pts',(18.8786271755125,-16.8398976801939,
1.7216066849587));
#171302=CARTESIAN_POINT('Ctrl Pts',(18.864366372587,-16.8389695167336,1.72076512015129));
#171303=CARTESIAN_POINT('Ctrl Pts',(18.8416552559231,-16.8377221486527,
1.7194184664676));
#171304=CARTESIAN_POINT('Ctrl Pts',(18.8332103846389,-16.8373090572752,
1.71891631930771));
#171305=CARTESIAN_POINT('Ctrl Pts',(18.818312422805,-16.8366697405475,1.71802788782991));
#171306=CARTESIAN_POINT('Ctrl Pts',(18.811860311207,-16.8364224283407,1.71764226963368));
#171307=CARTESIAN_POINT('Ctrl Pts',(18.7985130896356,-16.8359719650985,
1.71684275777739));
#171308=CARTESIAN_POINT('Ctrl Pts',(18.7916179238947,-16.835772990363,1.71642873780404));
#171309=CARTESIAN_POINT('Ctrl Pts',(18.7739166660637,-16.8353487577163,
1.71536326299231));
#171310=CARTESIAN_POINT('Ctrl Pts',(18.763109696509,-16.8351725529758,1.71471027884528));
#171311=CARTESIAN_POINT('Ctrl Pts',(18.7179999081334,-16.8347825527538,
1.71197394267123));
#171312=CARTESIAN_POINT('Ctrl Pts',(18.6836973667649,-16.8353197807208,
1.70986725341227));
#171313=CARTESIAN_POINT('Ctrl Pts',(18.5943673693626,-16.8388914215216,
1.70431027686346));
#171314=CARTESIAN_POINT('Ctrl Pts',(18.539421263544,-16.8432412583345,1.70082156104504));
#171315=CARTESIAN_POINT('Ctrl Pts',(18.3808407993589,-16.8620458663092,
1.69055706253802));
#171316=CARTESIAN_POINT('Ctrl Pts',(18.2780335179298,-16.8820431983753,
1.68365068975032));
#171317=CARTESIAN_POINT('Ctrl Pts',(18.0581328402662,-16.9419983944864,
1.66859016502744));
#171318=CARTESIAN_POINT('Ctrl Pts',(17.9421811055153,-16.98478555336,1.66046097023692));
#171319=CARTESIAN_POINT('Ctrl Pts',(17.8220692052393,-17.0414607256951,
1.65225898559873));
#171320=CARTESIAN_POINT('Ctrl Pts',(17.8135597146947,-17.045545756681,1.65167921893351));
#171321=CARTESIAN_POINT('Ctrl Pts',(17.8009716093122,-17.0516926822473,
1.6508238396777));
#171322=CARTESIAN_POINT('Ctrl Pts',(17.796872024498,-17.0537110235346,1.65054562693728));
#171323=CARTESIAN_POINT('Ctrl Pts',(17.7895805346866,-17.0573302071775,
1.65005148501018));
#171324=CARTESIAN_POINT('Ctrl Pts',(17.7863861209334,-17.0589258632729,
1.64983523806324));
#171325=CARTESIAN_POINT('Ctrl Pts',(17.7795905838122,-17.0623418438325,
1.64937572599234));
#171326=CARTESIAN_POINT('Ctrl Pts',(17.7759906352782,-17.0641643772275,
1.64913260219275));
#171327=CARTESIAN_POINT('Ctrl Pts',(17.766164494739,-17.0691743683178,1.6484697616433));
#171328=CARTESIAN_POINT('Ctrl Pts',(17.7599487897929,-17.072382441142,1.64805131888324));
#171329=CARTESIAN_POINT('Ctrl Pts',(17.7460917540264,-17.0796215838848,
1.64712010829601));
#171330=CARTESIAN_POINT('Ctrl Pts',(17.7384589252216,-17.0836687634402,
1.64660830029875));
#171331=CARTESIAN_POINT('Ctrl Pts',(17.7150040138148,-17.096289888059,1.64503839395978));
#171332=CARTESIAN_POINT('Ctrl Pts',(17.699265914446,-17.1050191512982,1.64398898820383));
#171333=CARTESIAN_POINT('Ctrl Pts',(17.6391124288452,-17.1393940195727,
1.63998604701163));
#171334=CARTESIAN_POINT('Ctrl Pts',(17.5955206089469,-17.1664511719524,
1.63710213117425));
#171335=CARTESIAN_POINT('Ctrl Pts',(17.4396156582002,-17.2712538083259,
1.62669260069816));
#171336=CARTESIAN_POINT('Ctrl Pts',(17.3339153733609,-17.3582296089895,
1.61942629536931));
#171337=CARTESIAN_POINT('Ctrl Pts',(17.1677260897055,-17.5243585953945,
1.60646827782242));
#171338=CARTESIAN_POINT('Ctrl Pts',(17.1030698550247,-17.5986939526255,
1.60092467288424));
#171339=CARTESIAN_POINT('Ctrl Pts',(17.0354279899442,-17.6883796259513,
1.59434072383888));
#171340=CARTESIAN_POINT('Ctrl Pts',(17.0271443287725,-17.699591509611,1.59351954304025));
#171341=CARTESIAN_POINT('Ctrl Pts',(17.0140751751975,-17.7176510349408,
1.59219943388756));
#171342=CARTESIAN_POINT('Ctrl Pts',(17.0092183520962,-17.7244467284401,
1.59170326642351));
#171343=CARTESIAN_POINT('Ctrl Pts',(17.0006880677466,-17.7365329181981,
1.59082177070814));
#171344=CARTESIAN_POINT('Ctrl Pts',(16.9969982740845,-17.7418117980301,
1.59043707512971));
#171345=CARTESIAN_POINT('Ctrl Pts',(16.9893819665393,-17.7528148182868,
1.58963584722513));
#171346=CARTESIAN_POINT('Ctrl Pts',(16.985459406972,-17.7585415903918,1.58921917062955));
#171347=CARTESIAN_POINT('Ctrl Pts',(16.9753908836527,-17.7733974005587,
1.58813909123413));
#171348=CARTESIAN_POINT('Ctrl Pts',(16.9692878714939,-17.7825551710961,
1.58747407750949));
#171349=CARTESIAN_POINT('Ctrl Pts',(16.943496282987,-17.8219179611135,1.58461871293199));
#171350=CARTESIAN_POINT('Ctrl Pts',(16.9245106312976,-17.8525742640169,
1.58240241153226));
#171351=CARTESIAN_POINT('Ctrl Pts',(16.8765273212873,-17.9346655813933,
1.57648341351698));
#171352=CARTESIAN_POINT('Ctrl Pts',(16.8488840145837,-17.9868519295412,
1.57273575394182));
#171353=CARTESIAN_POINT('Ctrl Pts',(16.7944907198973,-18.1008151574872,
1.56459391176849));
#171354=CARTESIAN_POINT('Ctrl Pts',(16.7684520761493,-18.1628105935934,
1.5601895301041));
#171355=CARTESIAN_POINT('Ctrl Pts',(16.7454191832631,-18.2258902732327,
1.55576066005867));
#171356=CARTESIAN_POINT('',(16.62007989375,-18.9528282577771,2.08900081341629));
#171357=CARTESIAN_POINT('Ctrl Pts',(16.7454193692336,-18.2258897639197,
1.33163196665472));
#171358=CARTESIAN_POINT('Ctrl Pts',(16.7469780089451,-18.2216211548481,
1.33190185432591));
#171359=CARTESIAN_POINT('Ctrl Pts',(16.7485503828935,-18.2173575917481,
1.33217219704567));
#171360=CARTESIAN_POINT('Ctrl Pts',(16.752380836381,-18.2070732661986,1.33282619209588));
#171361=CARTESIAN_POINT('Ctrl Pts',(16.7546526300675,-18.2010577012268,
1.33321029920865));
#171362=CARTESIAN_POINT('Ctrl Pts',(16.7594433952834,-18.1885448446607,
1.33401258755428));
#171363=CARTESIAN_POINT('Ctrl Pts',(16.7619671080003,-18.1820494622973,
1.33443092439066));
#171364=CARTESIAN_POINT('Ctrl Pts',(16.7686050699071,-18.1652118088885,
1.33552028607709));
#171365=CARTESIAN_POINT('Ctrl Pts',(16.7727688572223,-18.1548894141375,
1.33619297516802));
#171366=CARTESIAN_POINT('Ctrl Pts',(16.7912114292374,-18.110188050701,1.33912754616079));
#171367=CARTESIAN_POINT('Ctrl Pts',(16.8063135109684,-18.0761579407643,
1.34141720640058));
#171368=CARTESIAN_POINT('Ctrl Pts',(16.8488256589398,-17.9867963777953,
1.34758320257742));
#171369=CARTESIAN_POINT('Ctrl Pts',(16.8777709018602,-17.932238882343,1.35150931092493));
#171370=CARTESIAN_POINT('Ctrl Pts',(16.9832811504378,-17.7527838577309,
1.36495842800826));
#171371=CARTESIAN_POINT('Ctrl Pts',(17.0704045413428,-17.6345855675469,
1.37476374262784));
#171372=CARTESIAN_POINT('Ctrl Pts',(17.1821619049304,-17.5119067325975,
1.38559625226587));
#171373=CARTESIAN_POINT('Ctrl Pts',(17.1955076964967,-17.497657689187,1.38686501323907));
#171374=CARTESIAN_POINT('Ctrl Pts',(17.2456814202752,-17.4455518515892,
1.39153840666011));
#171375=CARTESIAN_POINT('Ctrl Pts',(17.2837281423924,-17.4088892563266,
1.39489463915846));
#171376=CARTESIAN_POINT('Ctrl Pts',(17.3295906039455,-17.3678917919831,
1.3986891918161));
#171377=CARTESIAN_POINT('Ctrl Pts',(17.3361072826765,-17.3621382062489,
1.39922271506066));
#171378=CARTESIAN_POINT('Ctrl Pts',(17.3460336267214,-17.3534824398874,
1.40002662231329));
#171379=CARTESIAN_POINT('Ctrl Pts',(17.3494172706136,-17.3505507470801,
1.40029912782608));
#171380=CARTESIAN_POINT('Ctrl Pts',(17.3555106795293,-17.3453049790022,
1.40078709230336));
#171381=CARTESIAN_POINT('Ctrl Pts',(17.3582169964169,-17.3429870029183,
1.40100283730247));
#171382=CARTESIAN_POINT('Ctrl Pts',(17.3641139356768,-17.337961996103,1.4014708084251));
#171383=CARTESIAN_POINT('Ctrl Pts',(17.3673067243892,-17.3352575967872,
1.40172284187846));
#171384=CARTESIAN_POINT('Ctrl Pts',(17.3763062231306,-17.3276804288929,
1.40242955523647));
#171385=CARTESIAN_POINT('Ctrl Pts',(17.3821311845605,-17.322829299732,1.40288267925102));
#171386=CARTESIAN_POINT('Ctrl Pts',(17.4172897232876,-17.293867063297,1.40559281551996));
#171387=CARTESIAN_POINT('Ctrl Pts',(17.4472435822403,-17.2705158003604,
1.40779849345484));
#171388=CARTESIAN_POINT('Ctrl Pts',(17.5483186251552,-17.1960041054724,
1.41496680558571));
#171389=CARTESIAN_POINT('Ctrl Pts',(17.621989712496,-17.1484486546492,1.41976115841988));
#171390=CARTESIAN_POINT('Ctrl Pts',(17.8507181970275,-17.0201611612989,
1.43402845205778));
#171391=CARTESIAN_POINT('Ctrl Pts',(18.0130018697045,-16.953915166998,1.44342145294553));
#171392=CARTESIAN_POINT('Ctrl Pts',(18.2038295264748,-16.9023317694933,
1.45490743175263));
#171393=CARTESIAN_POINT('Ctrl Pts',(18.2261829698051,-16.8966794924945,
1.45625813314429));
#171394=CARTESIAN_POINT('Ctrl Pts',(18.2579262536769,-16.8892023540638,
1.45818536421926));
#171395=CARTESIAN_POINT('Ctrl Pts',(18.2672434753156,-16.8870741703077,
1.45875214469973));
#171396=CARTESIAN_POINT('Ctrl Pts',(18.2824027876545,-16.8837194126031,
1.45967621774609));
#171397=CARTESIAN_POINT('Ctrl Pts',(18.2882362840617,-16.8824543158388,
1.46003227046598));
#171398=CARTESIAN_POINT('Ctrl Pts',(18.3004560173951,-16.8798583132181,
1.46077910342176));
#171399=CARTESIAN_POINT('Ctrl Pts',(18.3068432030002,-16.8785322225193,
1.46117003357874));
#171400=CARTESIAN_POINT('Ctrl Pts',(18.3220485566541,-16.8754485662721,
1.46210207030448));
#171401=CARTESIAN_POINT('Ctrl Pts',(18.330871940371,-16.8737176293311,1.46264402126151));
#171402=CARTESIAN_POINT('Ctrl Pts',(18.3606155311281,-16.8680791859027,
1.46447480585121));
#171403=CARTESIAN_POINT('Ctrl Pts',(18.3815830380425,-16.8644310420847,
1.4657718505232));
#171404=CARTESIAN_POINT('Ctrl Pts',(18.560027681871,-16.8361483419412,1.47686847813807));
#171405=CARTESIAN_POINT('Ctrl Pts',(18.7197391318618,-16.8290602832147,
1.48724159313066));
#171406=CARTESIAN_POINT('Ctrl Pts',(19.0099955999645,-16.8489463452772,
1.50645979812625));
#171407=CARTESIAN_POINT('Ctrl Pts',(19.1401771170331,-16.8701655909268,
1.5151976290909));
#171408=CARTESIAN_POINT('Ctrl Pts',(19.2827888655724,-16.9073074487044,
1.52439146147466));
#171409=CARTESIAN_POINT('Ctrl Pts',(19.2979796407365,-16.9114452110457,
1.52536556984897));
#171410=CARTESIAN_POINT('Ctrl Pts',(19.3187007994414,-16.9173384558227,
1.52668584074879));
#171411=CARTESIAN_POINT('Ctrl Pts',(19.3242717868769,-16.9189476534882,
1.52703995934182));
#171412=CARTESIAN_POINT('Ctrl Pts',(19.3331111279451,-16.921540321884,1.52760041106523));
#171413=CARTESIAN_POINT('Ctrl Pts',(19.3363837882496,-16.9225088272872,
1.52780760179939));
#171414=CARTESIAN_POINT('Ctrl Pts',(19.3431353839554,-16.924524652782,1.52823438145459));
#171415=CARTESIAN_POINT('Ctrl Pts',(19.3466139669554,-16.9255730145887,
1.52845390213702));
#171416=CARTESIAN_POINT('Ctrl Pts',(19.354892372933,-16.9280911928808,1.52897548174013));
#171417=CARTESIAN_POINT('Ctrl Pts',(19.3596897368803,-16.9295691476233,
1.52927706600975));
#171418=CARTESIAN_POINT('Ctrl Pts',(19.3758337328626,-16.9346056739562,
1.5302898239611));
#171419=CARTESIAN_POINT('Ctrl Pts',(19.3871558638069,-16.9382428548627,
1.53099654512627));
#171420=CARTESIAN_POINT('Ctrl Pts',(19.5221729641012,-16.9828749998802,
1.53938838433947));
#171421=CARTESIAN_POINT('Ctrl Pts',(19.6418773231725,-17.0351174996117,
1.54647743995801));
#171422=CARTESIAN_POINT('Ctrl Pts',(19.8981299046051,-17.1763819220244,
1.56237387340025));
#171423=CARTESIAN_POINT('Ctrl Pts',(20.0307355897197,-17.2707838276206,
1.57115663668387));
#171424=CARTESIAN_POINT('Ctrl Pts',(20.168878505492,-17.3952805290851,1.58195490276796));
#171425=CARTESIAN_POINT('Ctrl Pts',(20.1862331046894,-17.4114576346305,
1.58334411948527));
#171426=CARTESIAN_POINT('Ctrl Pts',(20.2102717720847,-17.4346325027105,
1.58531698577307));
#171427=CARTESIAN_POINT('Ctrl Pts',(20.2171857298994,-17.4413900063892,
1.58589024094843));
#171428=CARTESIAN_POINT('Ctrl Pts',(20.2283073981905,-17.4524099664384,
1.58682198497202));
#171429=CARTESIAN_POINT('Ctrl Pts',(20.2325437818724,-17.4566433864389,
1.5871791920608));
#171430=CARTESIAN_POINT('Ctrl Pts',(20.2413447944384,-17.4655132014424,
1.58792612371419));
#171431=CARTESIAN_POINT('Ctrl Pts',(20.2459061215589,-17.4701527711222,
1.58831598794524));
#171432=CARTESIAN_POINT('Ctrl Pts',(20.2566543663712,-17.4811866721208,
1.58924124341416));
#171433=CARTESIAN_POINT('Ctrl Pts',(20.2628224660245,-17.4875990888769,
1.5897774467552));
#171434=CARTESIAN_POINT('Ctrl Pts',(20.2832287960464,-17.5090831566346,
1.59156906342601));
#171435=CARTESIAN_POINT('Ctrl Pts',(20.2972856713562,-17.5243247073985,
1.59283221785415));
#171436=CARTESIAN_POINT('Ctrl Pts',(20.371130264684,-17.6067910760653,1.59962724714155));
#171437=CARTESIAN_POINT('Ctrl Pts',(20.4268036828167,-17.6775610479136,
1.60532712714341));
#171438=CARTESIAN_POINT('Ctrl Pts',(20.5546065910936,-17.8632259826244,
1.61993455285906));
#171439=CARTESIAN_POINT('Ctrl Pts',(20.6205227926009,-17.9819147995188,
1.62898784864941));
#171440=CARTESIAN_POINT('Ctrl Pts',(20.7047984212395,-18.1752519701093,
1.6427793589995));
#171441=CARTESIAN_POINT('Ctrl Pts',(20.7312360825949,-18.246001089841,1.64763738032002));
#171442=CARTESIAN_POINT('Ctrl Pts',(20.7566829422805,-18.3270737668287,
1.65288547815168));
#171443=CARTESIAN_POINT('Ctrl Pts',(20.7594644044671,-18.3361485277717,
1.6534684931989));
#171444=CARTESIAN_POINT('Ctrl Pts',(20.7634973863682,-18.3496294064328,
1.65432771863036));
#171445=CARTESIAN_POINT('Ctrl Pts',(20.7647957461813,-18.3540212282426,
1.65460656269733));
#171446=CARTESIAN_POINT('Ctrl Pts',(20.7670813031071,-18.3618456375569,
1.65510139107388));
#171447=CARTESIAN_POINT('Ctrl Pts',(20.7680740731972,-18.3652765370669,
1.65531769668012));
#171448=CARTESIAN_POINT('Ctrl Pts',(20.770190773628,-18.3726615575667,1.65578184656254));
#171449=CARTESIAN_POINT('Ctrl Pts',(20.7713118682925,-18.3766164327475,
1.65602952506099));
#171450=CARTESIAN_POINT('Ctrl Pts',(20.7743768450923,-18.3875499934551,
1.65671186958355));
#171451=CARTESIAN_POINT('Ctrl Pts',(20.7762964576538,-18.3945355057206,
1.65714514739522));
#171452=CARTESIAN_POINT('Ctrl Pts',(20.786651167271,-18.4329879646419,1.6595161752194));
#171453=CARTESIAN_POINT('Ctrl Pts',(20.79439540772,-18.4646383948966,1.66141638526182));
#171454=CARTESIAN_POINT('Ctrl Pts',(20.8364045223904,-18.6552897504772,
1.67262496741146));
#171455=CARTESIAN_POINT('Ctrl Pts',(20.85298602281,-18.817642977263,1.68122171408322));
#171456=CARTESIAN_POINT('Ctrl Pts',(20.8492485224996,-19.097127165588,1.69652342599794));
#171457=CARTESIAN_POINT('Ctrl Pts',(20.8380194334806,-19.2136011642474,
1.70304550944014));
#171458=CARTESIAN_POINT('Ctrl Pts',(20.8147014981872,-19.3426078253938,
1.71072561209554));
#171459=CARTESIAN_POINT('Ctrl Pts',(20.8120175439466,-19.356643386154,1.71156711253977));
#171460=CARTESIAN_POINT('Ctrl Pts',(20.8075197981348,-19.3789380834008,
1.7129136784744));
#171461=CARTESIAN_POINT('Ctrl Pts',(20.8057982323896,-19.3872155344412,
1.7134158027586));
#171462=CARTESIAN_POINT('Ctrl Pts',(20.8026745525841,-19.4017958257363,
1.71430420272433));
#171463=CARTESIAN_POINT('Ctrl Pts',(20.8012930918349,-19.408103015102,1.71468981237914));
#171464=CARTESIAN_POINT('Ctrl Pts',(20.7983761098417,-19.4211352259918,
1.71548931529257));
#171465=CARTESIAN_POINT('Ctrl Pts',(20.7968365309985,-19.4278592520668,
1.7159033349055));
#171466=CARTESIAN_POINT('Ctrl Pts',(20.7928002588448,-19.4450997082577,
1.7169688271686));
#171467=CARTESIAN_POINT('Ctrl Pts',(20.7902558605417,-19.4556046637053,
1.71762182929343));
#171468=CARTESIAN_POINT('Ctrl Pts',(20.7793001312434,-19.4993694674615,
1.72035839537104));
#171469=CARTESIAN_POINT('Ctrl Pts',(20.7701617717159,-19.5324403361604,
1.722465302016));
#171470=CARTESIAN_POINT('Ctrl Pts',(20.7442598175371,-19.6180191232367,
1.72802300249671));
#171471=CARTESIAN_POINT('Ctrl Pts',(20.7262429966346,-19.670117697727,1.73151223825882));
#171472=CARTESIAN_POINT('Ctrl Pts',(20.6664533298185,-19.8233674071083,
1.74208589180962));
#171473=CARTESIAN_POINT('Ctrl Pts',(20.6188535389836,-19.9220415974775,
1.74931868870912));
#171474=CARTESIAN_POINT('Ctrl Pts',(20.5394820030683,-20.0584679847767,
1.75974486664127));
#171475=CARTESIAN_POINT('Ctrl Pts',(20.5136850643191,-20.0995007510991,
1.76293918765385));
#171476=CARTESIAN_POINT('Ctrl Pts',(20.4766022627348,-20.15422202012,1.7672515224871));
#171477=CARTESIAN_POINT('Ctrl Pts',(20.4665197717848,-20.1687069065792,
1.76839817538964));
#171478=CARTESIAN_POINT('Ctrl Pts',(20.4252331100915,-20.2264668857623,
1.77298679902957));
#171479=CARTESIAN_POINT('Ctrl Pts',(20.3925765095485,-20.2686853361526,
1.77637829090998));
#171480=CARTESIAN_POINT('Ctrl Pts',(20.3527644317497,-20.3163191551136,
1.78020788443709));
#171481=CARTESIAN_POINT('Ctrl Pts',(20.3471307613491,-20.3229756362923,
1.78074310562718));
#171482=CARTESIAN_POINT('Ctrl Pts',(20.3385386736289,-20.3330013554091,
1.78154907719668));
#171483=CARTESIAN_POINT('Ctrl Pts',(20.3356104994851,-20.3363962249324,
1.78182196459178));
#171484=CARTESIAN_POINT('Ctrl Pts',(20.3303352547835,-20.3424731049659,
1.78231034749108));
#171485=CARTESIAN_POINT('Ctrl Pts',(20.3279921868627,-20.3451585014285,
1.78252613113583));
#171486=CARTESIAN_POINT('Ctrl Pts',(20.3228864021595,-20.3509805113537,
1.78299387618881));
#171487=CARTESIAN_POINT('Ctrl Pts',(20.3201211831963,-20.3541148537207,
1.78324564659638));
#171488=CARTESIAN_POINT('Ctrl Pts',(20.312328381068,-20.3628953455847,1.78395089266421));
#171489=CARTESIAN_POINT('Ctrl Pts',(20.3072797517182,-20.3685228488869,
1.78440282271366));
#171490=CARTESIAN_POINT('Ctrl Pts',(20.2769299784554,-20.4019900913812,
1.78709093366332));
#171491=CARTESIAN_POINT('Ctrl Pts',(20.250918878903,-20.429180317943,1.78927674428094));
#171492=CARTESIAN_POINT('Ctrl Pts',(20.1629639659735,-20.5163473506456,
1.79634826981673));
#171493=CARTESIAN_POINT('Ctrl Pts',(20.0980782206357,-20.5732382943573,
1.80107084203581));
#171494=CARTESIAN_POINT('Ctrl Pts',(19.8902352996053,-20.7341347677382,
1.81537497403396));
#171495=CARTESIAN_POINT('Ctrl Pts',(19.7376084161582,-20.8243375496902,
1.82486496392234));
#171496=CARTESIAN_POINT('Ctrl Pts',(19.5545390772695,-20.9036478593207,
1.83645921108515));
#171497=CARTESIAN_POINT('Ctrl Pts',(19.5333737533294,-20.9124120195365,
1.83780132308227));
#171498=CARTESIAN_POINT('Ctrl Pts',(19.5032057142976,-20.9243342608018,
1.83971837378418));
#171499=CARTESIAN_POINT('Ctrl Pts',(19.4943170104229,-20.9277777978266,
1.84028370387923));
#171500=CARTESIAN_POINT('Ctrl Pts',(19.4798293982838,-20.9332781437326,
1.84120604403086));
#171501=CARTESIAN_POINT('Ctrl Pts',(19.47424445741,-20.935371552768,1.84156182341835));
#171502=CARTESIAN_POINT('Ctrl Pts',(19.4625294868531,-20.9397063131477,
1.84230859847614));
#171503=CARTESIAN_POINT('Ctrl Pts',(19.4563977974758,-20.9419429693494,
1.84269974633753));
#171504=CARTESIAN_POINT('Ctrl Pts',(19.4417751703768,-20.9472003730462,
1.84363325480104));
#171505=CARTESIAN_POINT('Ctrl Pts',(19.4332751454164,-20.950195307642,1.844176467059));
#171506=CARTESIAN_POINT('Ctrl Pts',(19.4045222170771,-20.9601203050596,
1.84601605398008));
#171507=CARTESIAN_POINT('Ctrl Pts',(19.3841839186975,-20.9667972657927,
1.84732074829423));
#171508=CARTESIAN_POINT('Ctrl Pts',(19.2725577184012,-21.0015774263021,
1.85450266061469));
#171509=CARTESIAN_POINT('Ctrl Pts',(19.1795609380738,-21.0237826208264,
1.86057006010431));
#171510=CARTESIAN_POINT('Ctrl Pts',(18.9174225540787,-21.0679061201764,
1.87784605121419));
#171511=CARTESIAN_POINT('Ctrl Pts',(18.7466642970659,-21.0758029789536,
1.88933830324689));
#171512=CARTESIAN_POINT('Ctrl Pts',(18.5401936393751,-21.0604298124125,
1.90255187805656));
#171513=CARTESIAN_POINT('Ctrl Pts',(18.5036519322531,-21.0567511306786,
1.90486141653235));
#171514=CARTESIAN_POINT('Ctrl Pts',(18.4601413497464,-21.0512239957896,
1.90756231597942));
#171515=CARTESIAN_POINT('Ctrl Pts',(18.453065164394,-21.0502887232869,1.90800000670298));
#171516=CARTESIAN_POINT('Ctrl Pts',(18.4415246335658,-21.048703963245,1.9087111374922));
#171517=CARTESIAN_POINT('Ctrl Pts',(18.4370574615614,-21.0480759717136,
1.90898574517932));
#171518=CARTESIAN_POINT('Ctrl Pts',(18.4290627168522,-21.0469260056001,
1.9094759757948));
#171519=CARTESIAN_POINT('Ctrl Pts',(18.4255344373287,-21.0464093947568,
1.90969189644735));
#171520=CARTESIAN_POINT('Ctrl Pts',(18.4178939429926,-21.0452709468414,
1.91015853495268));
#171521=CARTESIAN_POINT('Ctrl Pts',(18.4137822631944,-21.0446459083862,
1.9104090693682));
#171522=CARTESIAN_POINT('Ctrl Pts',(18.4022962796745,-21.0428652172993,
1.91110737182983));
#171523=CARTESIAN_POINT('Ctrl Pts',(18.3949261227597,-21.0416826612019,
1.91155364281015));
#171524=CARTESIAN_POINT('Ctrl Pts',(18.3520512124472,-21.034570492711,1.9141400490475));
#171525=CARTESIAN_POINT('Ctrl Pts',(18.3166937771664,-21.0277746981841,
1.91623414697787));
#171526=CARTESIAN_POINT('Ctrl Pts',(18.203351803317,-21.0029765966068,1.92287097850404));
#171527=CARTESIAN_POINT('Ctrl Pts',(18.1262052594277,-20.9814531437156,
1.92727266053633));
#171528=CARTESIAN_POINT('Ctrl Pts',(17.8746327119347,-20.8956278623516,
1.94176357484675));
#171529=CARTESIAN_POINT('Ctrl Pts',(17.7074882150783,-20.8127710653322,
1.95169893338996));
#171530=CARTESIAN_POINT('Ctrl Pts',(17.5349718850057,-20.6968519498344,
1.96378745058492));
#171531=CARTESIAN_POINT('Ctrl Pts',(17.5168351163464,-20.684248925318,1.96508210270746));
#171532=CARTESIAN_POINT('Ctrl Pts',(17.4920320181413,-20.6664316922833,
1.96688735191551));
#171533=CARTESIAN_POINT('Ctrl Pts',(17.485194405452,-20.6614575394964,1.96738873627143));
#171534=CARTESIAN_POINT('Ctrl Pts',(17.473494033636,-20.6528382169013,1.96825320442167));
#171535=CARTESIAN_POINT('Ctrl Pts',(17.4686168003439,-20.6492127999031,
1.96861551828467));
#171536=CARTESIAN_POINT('Ctrl Pts',(17.45876149504,-20.641820914333,1.9693516682046));
#171537=CARTESIAN_POINT('Ctrl Pts',(17.453784339615,-20.6380533291271,1.96972554583959));
#171538=CARTESIAN_POINT('Ctrl Pts',(17.4422552536449,-20.6292456112844,
1.9705965441672));
#171539=CARTESIAN_POINT('Ctrl Pts',(17.4357160681656,-20.6241890322635,
1.97109431190644));
#171540=CARTESIAN_POINT('Ctrl Pts',(17.4220318999469,-20.6134787742574,
1.97214394385367));
#171541=CARTESIAN_POINT('Ctrl Pts',(17.4148934802356,-20.6078170183652,
1.97269612465169));
#171542=CARTESIAN_POINT('Ctrl Pts',(17.3959861783522,-20.5926210464096,
1.97417117336325));
#171543=CARTESIAN_POINT('Ctrl Pts',(17.3842828553074,-20.5830064424968,
1.97509725650284));
#171544=CARTESIAN_POINT('Ctrl Pts',(17.3489054577014,-20.5533013962361,
1.97793721926199));
#171545=CARTESIAN_POINT('Ctrl Pts',(17.3255701344935,-20.5328156784632,
1.97986693697989));
#171546=CARTESIAN_POINT('Ctrl Pts',(17.178583314136,-20.3979396385281,1.99239379582297));
#171547=CARTESIAN_POINT('Ctrl Pts',(17.0685229075891,-20.2696614622352,
2.00358061034142));
#171548=CARTESIAN_POINT('Ctrl Pts',(16.9197541441153,-20.0474479156722,
2.02119664031841));
#171549=CARTESIAN_POINT('Ctrl Pts',(16.8705007701706,-19.9613906267824,
2.0276487267251));
#171550=CARTESIAN_POINT('Ctrl Pts',(16.8232353237117,-19.8634611010547,
2.03436713444442));
#171551=CARTESIAN_POINT('Ctrl Pts',(16.8190812869546,-19.8547011230302,
2.03496280747162));
#171552=CARTESIAN_POINT('Ctrl Pts',(16.813036907456,-19.8417253150655,2.03583701398545));
#171553=CARTESIAN_POINT('Ctrl Pts',(16.8111000197589,-19.837531482279,2.03611831334073));
#171554=CARTESIAN_POINT('Ctrl Pts',(16.8076882727652,-19.8300802439078,
2.03661584705273));
#171555=CARTESIAN_POINT('Ctrl Pts',(16.8062079246769,-19.8268254112821,
2.03683241629388));
#171556=CARTESIAN_POINT('Ctrl Pts',(16.8030539897002,-19.8198439910867,
2.03729530315268));
#171557=CARTESIAN_POINT('Ctrl Pts',(16.8013829451207,-19.8161163158954,
2.037541464585));
#171558=CARTESIAN_POINT('Ctrl Pts',(16.7968258180321,-19.805871181523,2.03821535303689));
#171559=CARTESIAN_POINT('Ctrl Pts',(16.7939618142904,-19.7993438777717,
2.03864174812156));
#171560=CARTESIAN_POINT('Ctrl Pts',(16.77885106819,-19.7644269782842,2.04090763254381));
#171561=CARTESIAN_POINT('Ctrl Pts',(16.7671937064801,-19.7357845184199,
2.04271339922689));
#171562=CARTESIAN_POINT('Ctrl Pts',(16.7338151908354,-19.6483324993772,
2.048097605773));
#171563=CARTESIAN_POINT('Ctrl Pts',(16.714073417265,-19.5888013575638,2.0515893438376));
#171564=CARTESIAN_POINT('Ctrl Pts',(16.6439835862132,-19.3411372612689,
2.06573526128077));
#171565=CARTESIAN_POINT('Ctrl Pts',(16.6170670028625,-19.147403071309,2.07601658058645));
#171566=CARTESIAN_POINT('Ctrl Pts',(16.6170001249202,-18.9527272634281,
2.08722594301759));
#171567=CARTESIAN_POINT('Ctrl Pts',(16.7452305870807,-18.2258208582162,
2.13351566426921));
#171568=CARTESIAN_POINT('Ctrl Pts',(16.663115235549,-18.4580155040381,2.11869586918697));
#171569=CARTESIAN_POINT('Ctrl Pts',(16.6210475648562,-18.7055595715561,
2.10387607410474));
#171570=CARTESIAN_POINT('Ctrl Pts',(16.6201761380985,-18.9528314139021,
2.0890562790225));
#171571=CARTESIAN_POINT('Origin',(18.734,-18.952,0.));
#171572=CARTESIAN_POINT('',(16.7454192974523,-18.2258899605052,3.15472450021254));
#171573=CARTESIAN_POINT('',(16.7454193844899,-18.2258897221376,2.93545674301194));
#171574=CARTESIAN_POINT('',(16.7454193692319,-18.2258897639242,0.));
#171575=CARTESIAN_POINT('',(16.6170000449368,-18.9524361908011,3.11292713430694));
#171576=CARTESIAN_POINT('Ctrl Pts',(16.7454192974521,-18.225889960506,3.15472450021249));
#171577=CARTESIAN_POINT('Ctrl Pts',(16.6825885674479,-18.3979630216364,
3.14472560045024));
#171578=CARTESIAN_POINT('Ctrl Pts',(16.6422996473866,-18.5776169156608,
3.13494345590111));
#171579=CARTESIAN_POINT('Ctrl Pts',(16.6232302295293,-18.7874467506106,
3.12274999908918));
#171580=CARTESIAN_POINT('Ctrl Pts',(16.6212927654639,-18.8145415057395,
3.12116298812376));
#171581=CARTESIAN_POINT('Ctrl Pts',(16.6193445971276,-18.8518703054087,
3.11895644165119));
#171582=CARTESIAN_POINT('Ctrl Pts',(16.6188859031068,-18.8620790335503,
3.11835093317581));
#171583=CARTESIAN_POINT('Ctrl Pts',(16.6182717244293,-18.8783794128681,
3.1173806802683));
#171584=CARTESIAN_POINT('Ctrl Pts',(16.6180685939011,-18.8844691893339,
3.11701743262623));
#171585=CARTESIAN_POINT('Ctrl Pts',(16.6177137006794,-18.8966923162665,
3.11628677084266));
#171586=CARTESIAN_POINT('Ctrl Pts',(16.6175623043788,-18.9028256174748,
3.11591934881402));
#171587=CARTESIAN_POINT('Ctrl Pts',(16.6172825439101,-18.916583117471,3.11509337943087));
#171588=CARTESIAN_POINT('Ctrl Pts',(16.6171687079755,-18.9242074971486,
3.11463438114429));
#171589=CARTESIAN_POINT('Ctrl Pts',(16.6170306368061,-18.9387001093077,
3.11375948242246));
#171590=CARTESIAN_POINT('Ctrl Pts',(16.6169986298366,-18.945568170754,3.11334383289999));
#171591=CARTESIAN_POINT('Ctrl Pts',(16.6170000449368,-18.9524361908011,
3.11292713430694));
#171592=CARTESIAN_POINT('Ctrl Pts',(16.6170000447699,-18.9524353798984,
3.11292718350627));
#171593=CARTESIAN_POINT('Ctrl Pts',(16.6170022250297,-18.9630367189442,
3.11228397597961));
#171594=CARTESIAN_POINT('Ctrl Pts',(16.6170840379741,-18.9736377765493,
3.11163827929964));
#171595=CARTESIAN_POINT('Ctrl Pts',(16.6175725597191,-19.005714562482,3.10967678155756));
#171596=CARTESIAN_POINT('Ctrl Pts',(16.6182264799695,-19.0271845940186,
3.1083533681113));
#171597=CARTESIAN_POINT('Ctrl Pts',(16.6268700210254,-19.2163322797723,
3.0965992937741));
#171598=CARTESIAN_POINT('Ctrl Pts',(16.6544504544027,-19.3824913203712,
3.08554392257207));
#171599=CARTESIAN_POINT('Ctrl Pts',(16.7246641309952,-19.6237294021958,
3.06894891702627));
#171600=CARTESIAN_POINT('Ctrl Pts',(16.7526994568715,-19.7024005598765,
3.06345845456749));
#171601=CARTESIAN_POINT('Ctrl Pts',(16.7997273686543,-19.8131853824819,
3.05578051716473));
#171602=CARTESIAN_POINT('Ctrl Pts',(16.8150342368137,-19.8467746409251,
3.05346060512787));
#171603=CARTESIAN_POINT('Ctrl Pts',(16.8345081106732,-19.8867064188263,
3.05072704485781));
#171604=CARTESIAN_POINT('Ctrl Pts',(16.8378397184622,-19.8934466090163,
3.05026649507614));
#171605=CARTESIAN_POINT('Ctrl Pts',(16.8430751926107,-19.9038979815383,
3.04955386407448));
#171606=CARTESIAN_POINT('Ctrl Pts',(16.8449541986406,-19.9076214499039,
3.0493002755348));
#171607=CARTESIAN_POINT('Ctrl Pts',(16.8484596150504,-19.9145170981066,
3.048831231323));
#171608=CARTESIAN_POINT('Ctrl Pts',(16.8500830190775,-19.9176906941164,
3.04861559772222));
#171609=CARTESIAN_POINT('Ctrl Pts',(16.8537716962027,-19.9248569945028,
3.04812919544042));
#171610=CARTESIAN_POINT('Ctrl Pts',(16.8558416689543,-19.9288472196476,
3.04785872689899));
#171611=CARTESIAN_POINT('Ctrl Pts',(16.8619902175464,-19.9406078021087,
3.04706254392851));
#171612=CARTESIAN_POINT('Ctrl Pts',(16.8661044749617,-19.9483595362936,
3.04653902685531));
#171613=CARTESIAN_POINT('Ctrl Pts',(16.8962493750174,-20.0043129802856,
3.04276778266457));
#171614=CARTESIAN_POINT('Ctrl Pts',(16.9240964587281,-20.0515181831025,
3.03962703080612));
#171615=CARTESIAN_POINT('Ctrl Pts',(17.0437218103382,-20.2374160980352,
3.02720964487713));
#171616=CARTESIAN_POINT('Ctrl Pts',(17.1498597338429,-20.3661576374113,
3.0184523029206));
#171617=CARTESIAN_POINT('Ctrl Pts',(17.3134437142484,-20.5227737185384,
3.00590896696052));
#171618=CARTESIAN_POINT('Ctrl Pts',(17.3586625469145,-20.5625143033791,
3.00252826190643));
#171619=CARTESIAN_POINT('Ctrl Pts',(17.433970717374,-20.6232118508691,2.99697420538423));
#171620=CARTESIAN_POINT('Ctrl Pts',(17.4630191405319,-20.6454085758499,
2.99484900323994));
#171621=CARTESIAN_POINT('Ctrl Pts',(17.4992593892286,-20.6716428920851,
2.9922114452036));
#171622=CARTESIAN_POINT('Ctrl Pts',(17.5059201137793,-20.6764059389847,
2.99172724205299));
#171623=CARTESIAN_POINT('Ctrl Pts',(17.5188186126926,-20.6855169478644,
2.9907905697513));
#171624=CARTESIAN_POINT('Ctrl Pts',(17.5250525161715,-20.6898701883706,
2.99033831149573));
#171625=CARTESIAN_POINT('Ctrl Pts',(17.5313496175007,-20.6942172826115,
2.98988187391757));
#171626=CARTESIAN_POINT('Ctrl Pts',(17.5313895616197,-20.6942448553101,
2.98987897863404));
#171627=CARTESIAN_POINT('Ctrl Pts',(17.5314710796563,-20.6943011215885,
2.98987306996709));
#171628=CARTESIAN_POINT('Ctrl Pts',(17.5315126534155,-20.6943298148903,
2.98987005659652));
#171629=CARTESIAN_POINT('Ctrl Pts',(17.5315975383756,-20.694388396153,2.98986390395742));
#171630=CARTESIAN_POINT('Ctrl Pts',(17.5316408499326,-20.6944182841724,
2.98986076466458));
#171631=CARTESIAN_POINT('Ctrl Pts',(17.531729329459,-20.6944793363963,2.98985435156234));
#171632=CARTESIAN_POINT('Ctrl Pts',(17.5317744975197,-20.6945105004554,
2.98985107774799));
#171633=CARTESIAN_POINT('Ctrl Pts',(17.5318668207361,-20.6945741942869,
2.98984438613586));
#171634=CARTESIAN_POINT('Ctrl Pts',(17.5319139757756,-20.6946067237464,
2.98984096834838));
#171635=CARTESIAN_POINT('Ctrl Pts',(17.5320104154899,-20.694673245997,2.98983397846438));
#171636=CARTESIAN_POINT('Ctrl Pts',(17.5320597005397,-20.6947072387862,
2.9898304063428));
#171637=CARTESIAN_POINT('Ctrl Pts',(17.5321605587156,-20.6947767961784,
2.98982309631337));
#171638=CARTESIAN_POINT('Ctrl Pts',(17.5322121319455,-20.6948123605603,
2.98981935840036));
#171639=CARTESIAN_POINT('Ctrl Pts',(17.5323177412817,-20.694885180782,2.98981170412615));
#171640=CARTESIAN_POINT('Ctrl Pts',(17.5323717775328,-20.6949224363919,
2.9898077877571));
#171641=CARTESIAN_POINT('Ctrl Pts',(17.5324825070636,-20.6949987719184,
2.98979976250736));
#171642=CARTESIAN_POINT('Ctrl Pts',(17.5325392004475,-20.6950378515339,
2.98979565362213));
#171643=CARTESIAN_POINT('Ctrl Pts',(17.5326554600678,-20.6951179826989,
2.9897872277072));
#171644=CARTESIAN_POINT('Ctrl Pts',(17.5327150265564,-20.6951590339989,
2.98978291066263));
#171645=CARTESIAN_POINT('Ctrl Pts',(17.5328372738104,-20.6952432736158,
2.98977405094231));
#171646=CARTESIAN_POINT('Ctrl Pts',(17.5328999547889,-20.6952864615971,
2.98976950825501));
#171647=CARTESIAN_POINT('Ctrl Pts',(17.5330287015219,-20.6953751594731,
2.9897601776571));
#171648=CARTESIAN_POINT('Ctrl Pts',(17.5330947675712,-20.6954206690185,
2.98975538972957));
#171649=CARTESIAN_POINT('Ctrl Pts',(17.5332305891999,-20.6955142182559,
2.98974554657866));
#171650=CARTESIAN_POINT('Ctrl Pts',(17.5333003450219,-20.6955622574801,
2.98974049134279));
#171651=CARTESIAN_POINT('Ctrl Pts',(17.5334438906292,-20.6956611013263,
2.98973008862948));
#171652=CARTESIAN_POINT('Ctrl Pts',(17.5335176807041,-20.6957119054144,
2.98972474113693));
#171653=CARTESIAN_POINT('Ctrl Pts',(17.5336696860685,-20.695816546106,2.98971372557466));
#171654=CARTESIAN_POINT('Ctrl Pts',(17.5337479017288,-20.6958703821131,
2.98970805748486));
#171655=CARTESIAN_POINT('Ctrl Pts',(17.5339092045359,-20.6959813911893,
2.98969636840872));
#171656=CARTESIAN_POINT('Ctrl Pts',(17.5339922923074,-20.6960385636937,
2.98969034738505));
#171657=CARTESIAN_POINT('Ctrl Pts',(17.5341638523806,-20.696156595721,2.98967791528736));
#171658=CARTESIAN_POINT('Ctrl Pts',(17.5342523251175,-20.6962174543747,
2.98967150419113));
#171659=CARTESIAN_POINT('Ctrl Pts',(17.5344352467908,-20.6963432620896,
2.98965824910214));
#171660=CARTESIAN_POINT('Ctrl Pts',(17.5345296964249,-20.696408210248,2.98965140506984));
#171661=CARTESIAN_POINT('Ctrl Pts',(17.5347252610972,-20.6965426666279,
2.98963723420122));
#171662=CARTESIAN_POINT('Ctrl Pts',(17.534826376884,-20.6966121737155,2.98962990732363));
#171663=CARTESIAN_POINT('Ctrl Pts',(17.5350360728862,-20.696756292104,2.98961471290748));
#171664=CARTESIAN_POINT('Ctrl Pts',(17.5351446575342,-20.6968309044714,
2.98960684506337));
#171665=CARTESIAN_POINT('Ctrl Pts',(17.5353702472038,-20.6969858841434,
2.98959049949621));
#171666=CARTESIAN_POINT('Ctrl Pts',(17.5354872522772,-20.697066249085,2.98958202178857));
#171667=CARTESIAN_POINT('Ctrl Pts',(17.5407538962924,-20.7006828642732,
2.98920042853993));
#171668=CARTESIAN_POINT('Ctrl Pts',(17.5459191088559,-20.7041962842724,
2.98882645005517));
#171669=CARTESIAN_POINT('Ctrl Pts',(17.5578167486092,-20.7122123616813,
2.98796559034042));
#171670=CARTESIAN_POINT('Ctrl Pts',(17.5645595852529,-20.7166993263948,
2.98747812393825));
#171671=CARTESIAN_POINT('Ctrl Pts',(17.5843393157514,-20.7296984352639,
2.98604928024905));
#171672=CARTESIAN_POINT('Ctrl Pts',(17.5974443550221,-20.7381054451487,
2.9851039976049));
#171673=CARTESIAN_POINT('Ctrl Pts',(17.7099515808651,-20.8085403365685,
2.97699895964382));
#171674=CARTESIAN_POINT('Ctrl Pts',(17.8142360536012,-20.8623516958022,
2.96953654984386));
#171675=CARTESIAN_POINT('Ctrl Pts',(18.0737247741335,-20.970059161614,2.95118250552068));
#171676=CARTESIAN_POINT('Ctrl Pts',(18.2318032766922,-21.0150862433738,
2.94014783735797));
#171677=CARTESIAN_POINT('Ctrl Pts',(18.4243168587293,-21.046459545984,2.92776874172154));
#171678=CARTESIAN_POINT('Ctrl Pts',(18.4552515476172,-21.05080060463,2.92581301379045));
#171679=CARTESIAN_POINT('Ctrl Pts',(18.4933740750363,-21.0552924885962,
2.9234529893992));
#171680=CARTESIAN_POINT('Ctrl Pts',(18.5004796703129,-21.0560932458748,
2.92301524173163));
#171681=CARTESIAN_POINT('Ctrl Pts',(18.5116558727195,-21.0572954228324,
2.9223302171848));
#171682=CARTESIAN_POINT('Ctrl Pts',(18.5157237422032,-21.0577210651632,
2.92208161212249));
#171683=CARTESIAN_POINT('Ctrl Pts',(18.5233493923546,-21.0584966416467,
2.92161697124014));
#171684=CARTESIAN_POINT('Ctrl Pts',(18.5269067848668,-21.0588493492011,
2.92140078730138));
#171685=CARTESIAN_POINT('Ctrl Pts',(18.5350553507079,-21.0596364233856,
2.92090688910949));
#171686=CARTESIAN_POINT('Ctrl Pts',(18.5396470532403,-21.0600647996853,
2.92062951419674));
#171687=CARTESIAN_POINT('Ctrl Pts',(18.5538555186243,-21.0613435399777,
2.9197740045458));
#171688=CARTESIAN_POINT('Ctrl Pts',(18.5634768814921,-21.0621431415533,
2.91919864615131));
#171689=CARTESIAN_POINT('Ctrl Pts',(18.679751574077,-21.071005894935,2.91228955166938));
#171690=CARTESIAN_POINT('Ctrl Pts',(18.7868778260515,-21.0710420222558,
2.90636861251406));
#171691=CARTESIAN_POINT('Ctrl Pts',(19.002296397891,-21.0547594131499,2.89457347805691));
#171692=CARTESIAN_POINT('Ctrl Pts',(19.1102328110118,-21.0381516511517,
2.88871625187452));
#171693=CARTESIAN_POINT('Ctrl Pts',(19.2773963386886,-20.9990301871559,
2.87922429213375));
#171694=CARTESIAN_POINT('Ctrl Pts',(19.3377161140119,-20.9820586529281,
2.87571161218853));
#171695=CARTESIAN_POINT('Ctrl Pts',(19.4208385937325,-20.9546387004679,
2.87069003399091));
#171696=CARTESIAN_POINT('Ctrl Pts',(19.4443451908838,-20.9464218849405,
2.8692493709782));
#171697=CARTESIAN_POINT('Ctrl Pts',(19.4852470126977,-20.9313096843253,
2.86670306722439));
#171698=CARTESIAN_POINT('Ctrl Pts',(19.5027061747419,-20.9245946578616,
2.86560335020493));
#171699=CARTESIAN_POINT('Ctrl Pts',(19.5279989910008,-20.9144799255535,
2.86399053128551));
#171700=CARTESIAN_POINT('Ctrl Pts',(19.5359049942336,-20.9112626758244,
2.86348357151803));
#171701=CARTESIAN_POINT('Ctrl Pts',(19.5497473798616,-20.9055318703265,
2.86259088837445));
#171702=CARTESIAN_POINT('Ctrl Pts',(19.5556921762052,-20.9030388315656,
2.86220586459655));
#171703=CARTESIAN_POINT('Ctrl Pts',(19.5672246053783,-20.8981404788841,
2.86145569956698));
#171704=CARTESIAN_POINT('Ctrl Pts',(19.5728134449076,-20.8957381536617,
2.86109066318479));
#171705=CARTESIAN_POINT('Ctrl Pts',(19.5861670492308,-20.8899298779716,
2.86021485588539));
#171706=CARTESIAN_POINT('Ctrl Pts',(19.5939218130015,-20.8865013217834,
2.8597033149281));
#171707=CARTESIAN_POINT('Ctrl Pts',(19.6219376442148,-20.8739131477901,
2.85784445759871));
#171708=CARTESIAN_POINT('Ctrl Pts',(19.6420741322782,-20.8644812989342,
2.85648781670395));
#171709=CARTESIAN_POINT('Ctrl Pts',(19.8277496371534,-20.7739181608982,
2.84378166931708));
#171710=CARTESIAN_POINT('Ctrl Pts',(19.9821459063725,-20.6718194051452,
2.83164504671176));
#171711=CARTESIAN_POINT('Ctrl Pts',(20.182499044718,-20.4979935084846,2.81413070795178));
#171712=CARTESIAN_POINT('Ctrl Pts',(20.2405697501656,-20.4414612253418,
2.80880858474812));
#171713=CARTESIAN_POINT('Ctrl Pts',(20.3197446190823,-20.355002902914,2.80133393154705));
#171714=CARTESIAN_POINT('Ctrl Pts',(20.3435381823394,-20.3276417944048,
2.79905603609559));
#171715=CARTESIAN_POINT('Ctrl Pts',(20.3713803464612,-20.2939130172494,
2.79636523895101));
#171716=CARTESIAN_POINT('Ctrl Pts',(20.3761113533266,-20.2881194751797,
2.79590709477342));
#171717=CARTESIAN_POINT('Ctrl Pts',(20.383427127724,-20.2790631011196,2.79519737228355));
#171718=CARTESIAN_POINT('Ctrl Pts',(20.3860330915894,-20.2758175814692,
2.7949443060006));
#171719=CARTESIAN_POINT('Ctrl Pts',(20.3908536521749,-20.2697775565185,
2.7944757383486));
#171720=CARTESIAN_POINT('Ctrl Pts',(20.3930707401206,-20.2669851682601,
2.79426006213776));
#171721=CARTESIAN_POINT('Ctrl Pts',(20.3980740509156,-20.2606507788525,
2.79377294296695));
#171722=CARTESIAN_POINT('Ctrl Pts',(20.4008560179591,-20.2571054839278,
2.7935018039628));
#171723=CARTESIAN_POINT('Ctrl Pts',(20.4092349650928,-20.2463569919747,
2.79268419818449));
#171724=CARTESIAN_POINT('Ctrl Pts',(20.4147968133262,-20.2391263690934,
2.79214016406456));
#171725=CARTESIAN_POINT('Ctrl Pts',(20.45741557681,-20.1829729355585,2.78795918091646));
#171726=CARTESIAN_POINT('Ctrl Pts',(20.4923796339441,-20.132490647179,2.78445672779228));
#171727=CARTESIAN_POINT('Ctrl Pts',(20.5373985768837,-20.0610421607798,
2.7797373938508));
#171728=CARTESIAN_POINT('Ctrl Pts',(20.5493742954183,-20.0413287633696,
2.7784590303652));
#171729=CARTESIAN_POINT('Ctrl Pts',(20.5786288223331,-19.991349696965,2.77526747690636));
#171730=CARTESIAN_POINT('Ctrl Pts',(20.59548704035,-19.9608455649869,2.77336403134532));
#171731=CARTESIAN_POINT('Ctrl Pts',(20.6620560799351,-19.8330369165261,
2.765518731364));
#171732=CARTESIAN_POINT('Ctrl Pts',(20.7049493611461,-19.7323742801806,
2.75963513570466));
#171733=CARTESIAN_POINT('Ctrl Pts',(20.7574649984156,-19.5767426096472,
2.75050124773808));
#171734=CARTESIAN_POINT('Ctrl Pts',(20.7730110518191,-19.5239678457783,
2.74739971936568));
#171735=CARTESIAN_POINT('Ctrl Pts',(20.7948769375166,-19.4374367387551,
2.74226473750703));
#171736=CARTESIAN_POINT('Ctrl Pts',(20.8024619860172,-19.4040258793036,
2.74027049059516));
#171737=CARTESIAN_POINT('Ctrl Pts',(20.81136813513,-19.3598570084272,2.73761311955608));
#171738=CARTESIAN_POINT('Ctrl Pts',(20.8134223670016,-19.3492509549918,
2.73697344986146));
#171739=CARTESIAN_POINT('Ctrl Pts',(20.8166548922365,-19.3318488741907,
2.73592115569512));
#171740=CARTESIAN_POINT('Ctrl Pts',(20.8178813256869,-19.325061906529,2.73551007013574));
#171741=CARTESIAN_POINT('Ctrl Pts',(20.820191767646,-19.3119091634109,2.73471204373013));
#171742=CARTESIAN_POINT('Ctrl Pts',(20.8212798594306,-19.3055441758585,
2.73432523772691));
#171743=CARTESIAN_POINT('Ctrl Pts',(20.8237258358166,-19.2908310290024,
2.73342963665734));
#171744=CARTESIAN_POINT('Ctrl Pts',(20.8250628390276,-19.2824795532087,
2.73292018443606));
#171745=CARTESIAN_POINT('Ctrl Pts',(20.8285257277111,-19.2599861791992,
2.73154502349755));
#171746=CARTESIAN_POINT('Ctrl Pts',(20.8305583919263,-19.245830570418,2.73067638105955));
#171747=CARTESIAN_POINT('Ctrl Pts',(20.8479958613787,-19.1149853545658,
2.72261623137109));
#171748=CARTESIAN_POINT('Ctrl Pts',(20.8537848986482,-18.9972409174073,
2.71511830076217));
#171749=CARTESIAN_POINT('Ctrl Pts',(20.8441721744735,-18.7161641160448,
2.69674208479173));
#171750=CARTESIAN_POINT('Ctrl Pts',(20.8196541810789,-18.5538892504222,
2.68572495911518));
#171751=CARTESIAN_POINT('Ctrl Pts',(20.7685610741576,-18.3661584555948,
2.67338014168731));
#171752=CARTESIAN_POINT('Ctrl Pts',(20.7597681652363,-18.3364411847877,
2.67144021072281));
#171753=CARTESIAN_POINT('Ctrl Pts',(20.7481520750229,-18.3001324569244,
2.66909654633523));
#171754=CARTESIAN_POINT('Ctrl Pts',(20.7459443127011,-18.2933498948886,
2.6686598971194));
#171755=CARTESIAN_POINT('Ctrl Pts',(20.7424179167721,-18.2826994935451,
2.66797620444898));
#171756=CARTESIAN_POINT('Ctrl Pts',(20.7411223163095,-18.2788241653349,
2.66772784120054));
#171757=CARTESIAN_POINT('Ctrl Pts',(20.7386719872702,-18.2715648393806,
2.66726340508465));
#171758=CARTESIAN_POINT('Ctrl Pts',(20.7375199194272,-18.268180055116,2.66704718556748));
#171759=CARTESIAN_POINT('Ctrl Pts',(20.7348602790374,-18.2604304319294,
2.66655288313381));
#171760=CARTESIAN_POINT('Ctrl Pts',(20.7333469993902,-18.2560676033788,
2.66627514163402));
#171761=CARTESIAN_POINT('Ctrl Pts',(20.7286153688591,-18.2425689962341,
2.66541737359719));
#171762=CARTESIAN_POINT('Ctrl Pts',(20.7253485336115,-18.2334501795088,
2.66484014460777));
#171763=CARTESIAN_POINT('Ctrl Pts',(20.6858951203199,-18.1256585722324,
2.65803970026558));
#171764=CARTESIAN_POINT('Ctrl Pts',(20.6424663477042,-18.0297760990913,
2.65221478087934));
#171765=CARTESIAN_POINT('Ctrl Pts',(20.5855435632494,-17.9255196352191,
2.64572572656275));
#171766=CARTESIAN_POINT('Ctrl Pts',(20.5788832193334,-17.9135966983824,
2.64498128901625));
#171767=CARTESIAN_POINT('Ctrl Pts',(20.5179603780658,-17.8069729576078,
2.63829625911225));
#171768=CARTESIAN_POINT('Ctrl Pts',(20.4565657209145,-17.7165373384018,
2.63241820522035));
#171769=CARTESIAN_POINT('Ctrl Pts',(20.3414486534027,-17.5723335540748,
2.62215631898869));
#171770=CARTESIAN_POINT('Ctrl Pts',(20.2913141260961,-17.5159841003951,
2.61788266432365));
#171771=CARTESIAN_POINT('Ctrl Pts',(20.2250197954931,-17.4490347937054,
2.6123815893783));
#171772=CARTESIAN_POINT('Ctrl Pts',(20.2115762521096,-17.4358163610347,
2.61127332060569));
#171773=CARTESIAN_POINT('Ctrl Pts',(20.1917729641286,-17.4168582132912,
2.60965024706848));
#171774=CARTESIAN_POINT('Ctrl Pts',(20.1855518603284,-17.4109745252804,
2.60914169682538));
#171775=CARTESIAN_POINT('Ctrl Pts',(20.1745819219193,-17.4007249320977,
2.60824717684863));
#171776=CARTESIAN_POINT('Ctrl Pts',(20.1698484793457,-17.3963426620894,
2.60786191582327));
#171777=CARTESIAN_POINT('Ctrl Pts',(20.1606182665033,-17.3878752510172,
2.60711200543058));
#171778=CARTESIAN_POINT('Ctrl Pts',(20.1561237897811,-17.3837876948438,
2.60674746430017));
#171779=CARTESIAN_POINT('Ctrl Pts',(20.1453372274603,-17.3740622298702,
2.60587400540248));
#171780=CARTESIAN_POINT('Ctrl Pts',(20.1390289012606,-17.3684425620132,
2.60536432684467));
#171781=CARTESIAN_POINT('Ctrl Pts',(20.1161426816158,-17.3482991640617,
2.60351923789597));
#171782=CARTESIAN_POINT('Ctrl Pts',(20.0993723088522,-17.3339971680744,
2.60217468194046));
#171783=CARTESIAN_POINT('Ctrl Pts',(19.9387526562964,-17.201294121327,2.58936258085404));
#171784=CARTESIAN_POINT('Ctrl Pts',(19.7801118280689,-17.1021291511251,
2.57708863402808));
#171785=CARTESIAN_POINT('Ctrl Pts',(19.538064799707,-16.9920209717671,2.55953366432519));
#171786=CARTESIAN_POINT('Ctrl Pts',(19.46372609483,-16.9631461789141,2.55429956198979));
#171787=CARTESIAN_POINT('Ctrl Pts',(19.3537842034838,-16.9274394014562,
2.54693163888659));
#171788=CARTESIAN_POINT('Ctrl Pts',(19.319357300205,-16.9172186206141,2.54467610132618));
#171789=CARTESIAN_POINT('Ctrl Pts',(19.2774829604783,-16.9059377080309,
2.54200809273293));
#171790=CARTESIAN_POINT('Ctrl Pts',(19.2702707811739,-16.904035575501,2.5415512507225));
#171791=CARTESIAN_POINT('Ctrl Pts',(19.2590228645242,-16.901132554835,2.54084310303985));
#171792=CARTESIAN_POINT('Ctrl Pts',(19.2549940595747,-16.9001053934266,
2.54059031982601));
#171793=CARTESIAN_POINT('Ctrl Pts',(19.2475041557527,-16.8982192915258,
2.54012200912461));
#171794=CARTESIAN_POINT('Ctrl Pts',(19.2440439456601,-16.89735723537,2.53990630847174));
#171795=CARTESIAN_POINT('Ctrl Pts',(19.2361999560249,-16.8954240670267,
2.53941879458008));
#171796=CARTESIAN_POINT('Ctrl Pts',(19.2318149312573,-16.8943582286996,
2.53914728739158));
#171797=CARTESIAN_POINT('Ctrl Pts',(19.2204802964674,-16.8916415500104,
2.53844805517652));
#171798=CARTESIAN_POINT('Ctrl Pts',(19.2135256145716,-16.8900118308931,
2.53802151593928));
#171799=CARTESIAN_POINT('Ctrl Pts',(19.1706862598238,-16.8802015714935,
2.53540870784108));
#171800=CARTESIAN_POINT('Ctrl Pts',(19.1345991930462,-16.8729222544657,
2.53327055520097));
#171801=CARTESIAN_POINT('Ctrl Pts',(18.9307442695811,-16.8373071686671,
2.5214508932242));
#171802=CARTESIAN_POINT('Ctrl Pts',(18.7602171151967,-16.8283336627272,
2.51249780650082));
#171803=CARTESIAN_POINT('Ctrl Pts',(18.4950785314615,-16.8463548335748,
2.49788073300969));
#171804=CARTESIAN_POINT('Ctrl Pts',(18.4002748024625,-16.8592865843129,
2.49252205204228));
#171805=CARTESIAN_POINT('Ctrl Pts',(18.2857022869779,-16.8828995382233,
2.48571044764722));
#171806=CARTESIAN_POINT('Ctrl Pts',(18.264796443625,-16.887539892951,2.48445395202637));
#171807=CARTESIAN_POINT('Ctrl Pts',(18.2351963409351,-16.8945828923915,
2.48265413975129));
#171808=CARTESIAN_POINT('Ctrl Pts',(18.2264410654274,-16.8967252813588,
2.48211918534306));
#171809=CARTESIAN_POINT('Ctrl Pts',(18.2113698161335,-16.9005153439258,
2.48119373180126));
#171810=CARTESIAN_POINT('Ctrl Pts',(18.2050472433013,-16.9021364477347,
2.48080409521172));
#171811=CARTESIAN_POINT('Ctrl Pts',(18.1929620546896,-16.905294717921,2.48005661293148));
#171812=CARTESIAN_POINT('Ctrl Pts',(18.1871982315017,-16.9068270501516,
2.47969892721987));
#171813=CARTESIAN_POINT('Ctrl Pts',(18.1722406854964,-16.910871315506,2.47876758241382));
#171814=CARTESIAN_POINT('Ctrl Pts',(18.1630573890821,-16.9134209938077,
2.47819270160492));
#171815=CARTESIAN_POINT('Ctrl Pts',(18.1318711139857,-16.9223069000896,
2.47622976533447));
#171816=CARTESIAN_POINT('Ctrl Pts',(18.1099544456703,-16.9289378762109,
2.47483215058254));
#171817=CARTESIAN_POINT('Ctrl Pts',(17.9197966134086,-16.9898548796847,
2.4625428166505));
#171818=CARTESIAN_POINT('Ctrl Pts',(17.7588914191062,-17.064652670673,2.45093563248813));
#171819=CARTESIAN_POINT('Ctrl Pts',(17.5362353967373,-17.2042975253663,
2.43357171418553));
#171820=CARTESIAN_POINT('Ctrl Pts',(17.4661401486803,-17.2544614067884,
2.42789875448704));
#171821=CARTESIAN_POINT('Ctrl Pts',(17.3701109788857,-17.3324602412783,
2.42000164294333));
#171822=CARTESIAN_POINT('Ctrl Pts',(17.3415646015901,-17.3569368801045,
2.41763725416295));
#171823=CARTESIAN_POINT('Ctrl Pts',(17.3080783863316,-17.3872336646701,
2.41485851446678));
#171824=CARTESIAN_POINT('Ctrl Pts',(17.3025004899274,-17.3923348791717,
2.41439547564632));
#171825=CARTESIAN_POINT('Ctrl Pts',(17.2938809665726,-17.4003029815971,
2.41367983629214));
#171826=CARTESIAN_POINT('Ctrl Pts',(17.2908203712559,-17.4031491268571,
2.41342570830669));
#171827=CARTESIAN_POINT('Ctrl Pts',(17.2851655106111,-17.408439076604,2.41295616843403));
#171828=CARTESIAN_POINT('Ctrl Pts',(17.282569010505,-17.4108803469855,2.41274057543805));
#171829=CARTESIAN_POINT('Ctrl Pts',(17.276719833283,-17.4164077302856,2.41225489818765));
#171830=CARTESIAN_POINT('Ctrl Pts',(17.2734707971798,-17.4194976177268,
2.41198511019559));
#171831=CARTESIAN_POINT('Ctrl Pts',(17.2639302636739,-17.4286287227468,
2.41119278340234));
#171832=CARTESIAN_POINT('Ctrl Pts',(17.2576661687805,-17.4346986117645,
2.4106724103148));
#171833=CARTESIAN_POINT('Ctrl Pts',(17.2133345236271,-17.4781903077165,
2.40698703341621));
#171834=CARTESIAN_POINT('Ctrl Pts',(17.17665347041,-17.5170047706333,2.40392354355281));
#171835=CARTESIAN_POINT('Ctrl Pts',(17.1324647402756,-17.5674564393888,
2.40015193226831));
#171836=CARTESIAN_POINT('Ctrl Pts',(17.1235531461743,-17.5778322511852,
2.39938689918319));
#171837=CARTESIAN_POINT('Ctrl Pts',(17.0811122472264,-17.6282263481393,
2.39571809797011));
#171838=CARTESIAN_POINT('Ctrl Pts',(17.04896934407,-17.6693906766026,2.3928615223131));
#171839=CARTESIAN_POINT('Ctrl Pts',(16.9542698348109,-17.8003821168439,
2.38406088976791));
#171840=CARTESIAN_POINT('Ctrl Pts',(16.8971323202139,-17.893898179805,2.37816903274667));
#171841=CARTESIAN_POINT('Ctrl Pts',(16.8130787851647,-18.0589719260448,
2.36786971883574));
#171842=CARTESIAN_POINT('Ctrl Pts',(16.7823335504142,-18.1283290864511,
2.36357208491561));
#171843=CARTESIAN_POINT('Ctrl Pts',(16.751997197966,-18.2080617122727,2.3585915450917));
#171844=CARTESIAN_POINT('Ctrl Pts',(16.7486782220989,-18.2169648219953,
2.35803490618603));
#171845=CARTESIAN_POINT('Ctrl Pts',(16.7454193691877,-18.2258897640453,
2.35747631421306));
#171846=CARTESIAN_POINT('',(16.618038032075,-18.9501158127103,2.8890562790225));
#171847=CARTESIAN_POINT('Ctrl Pts',(16.618038032075,-18.9501158127103,2.8890562790225));
#171848=CARTESIAN_POINT('Ctrl Pts',(16.6223668846964,-19.4559949565256,
2.85866010167885));
#171849=CARTESIAN_POINT('Ctrl Pts',(17.0578065183866,-20.6740880083468,
2.78587198877473));
#171850=CARTESIAN_POINT('Ctrl Pts',(19.0938031538723,-21.4292709570805,
2.67069194031012));
#171851=CARTESIAN_POINT('Ctrl Pts',(21.0117474660562,-19.9903622879567,
2.54351613362868));
#171852=CARTESIAN_POINT('Ctrl Pts',(20.8399998530167,-17.5988206232279,
2.41634032694726));
#171853=CARTESIAN_POINT('Ctrl Pts',(18.7361280842055,-16.4487371345171,
2.28916452026581));
#171854=CARTESIAN_POINT('Ctrl Pts',(17.1750895514748,-17.2986361860363,
2.19488963270647));
#171855=CARTESIAN_POINT('Ctrl Pts',(16.7978195835484,-18.0771168317319,
2.1430066807076));
#171856=CARTESIAN_POINT('Ctrl Pts',(16.7452305870807,-18.2258208582162,
2.13351566426921));
#171857=CARTESIAN_POINT('Ctrl Pts',(16.617000874474,-18.950075806071,2.88845972223463));
#171858=CARTESIAN_POINT('Ctrl Pts',(16.6171407059199,-18.7962331792496,
2.8985386370441));
#171859=CARTESIAN_POINT('Ctrl Pts',(16.6340491292001,-18.6428594303531,
2.90887454244536));
#171860=CARTESIAN_POINT('Ctrl Pts',(16.6744827097124,-18.4609467005497,
2.92071560516971));
#171861=CARTESIAN_POINT('Ctrl Pts',(16.6822627059619,-18.4293919667833,
2.92275211774186));
#171862=CARTESIAN_POINT('Ctrl Pts',(16.6926607588507,-18.3910405538783,
2.92519558983202));
#171863=CARTESIAN_POINT('Ctrl Pts',(16.6945908013807,-18.3840638048843,
2.92563880153013));
#171864=CARTESIAN_POINT('Ctrl Pts',(16.697672606106,-18.3731419582713,2.92633044865512));
#171865=CARTESIAN_POINT('Ctrl Pts',(16.6988001139795,-18.3691901577678,
2.92658025432378));
#171866=CARTESIAN_POINT('Ctrl Pts',(16.7009291430241,-18.361809650113,2.92704592485674));
#171867=CARTESIAN_POINT('Ctrl Pts',(16.7019278235753,-18.358380232291,2.92726194509871));
#171868=CARTESIAN_POINT('Ctrl Pts',(16.7042273459033,-18.3505575968172,
2.92775389547489));
#171869=CARTESIAN_POINT('Ctrl Pts',(16.7055337702709,-18.3461660727402,
2.92802949632064));
#171870=CARTESIAN_POINT('Ctrl Pts',(16.7095931435689,-18.3326808968913,
2.92887412508428));
#171871=CARTESIAN_POINT('Ctrl Pts',(16.7123931058315,-18.3236013646558,
2.92944047766867));
#171872=CARTESIAN_POINT('Ctrl Pts',(16.7246572679426,-18.284762445607,2.93185432508154));
#171873=CARTESIAN_POINT('Ctrl Pts',(16.7347152088544,-18.2552049884584,
2.93366911664583));
#171874=CARTESIAN_POINT('Ctrl Pts',(16.7454193844899,-18.2258897221376,
2.93545674301194));
#171875=CARTESIAN_POINT('Origin',(18.734,-18.952,0.));
#171876=CARTESIAN_POINT('',(16.7454192997072,-18.22588995433,3.95421655704364));
#171877=CARTESIAN_POINT('',(16.7454193692324,-18.225889763923,3.73234496387082));
#171878=CARTESIAN_POINT('',(16.7454193692319,-18.2258897639242,0.));
#171879=CARTESIAN_POINT('Ctrl Pts',(16.7454192997072,-18.22588995433,3.95421655704364));
#171880=CARTESIAN_POINT('Ctrl Pts',(16.7247484957261,-18.2825006046045,
3.95029630227183));
#171881=CARTESIAN_POINT('Ctrl Pts',(16.7064930198954,-18.3399995059724,
3.94643457592769));
#171882=CARTESIAN_POINT('Ctrl Pts',(16.6875909790288,-18.4097441828717,
3.94195339820002));
#171883=CARTESIAN_POINT('Ctrl Pts',(16.6845683665288,-18.4212823282768,
3.94121862404921));
#171884=CARTESIAN_POINT('Ctrl Pts',(16.6804108712761,-18.4377180258621,
3.94018187945989));
#171885=CARTESIAN_POINT('Ctrl Pts',(16.6791957315543,-18.4425947800532,
3.93987549555571));
#171886=CARTESIAN_POINT('Ctrl Pts',(16.6771318961882,-18.451005180075,3.93934929254021));
#171887=CARTESIAN_POINT('Ctrl Pts',(16.6762749150324,-18.4545367535743,
3.93912899956492));
#171888=CARTESIAN_POINT('Ctrl Pts',(16.6746311950524,-18.4613873629827,
3.93870297479797));
#171889=CARTESIAN_POINT('Ctrl Pts',(16.6738433838323,-18.4647060931702,
3.9384971791502));
#171890=CARTESIAN_POINT('Ctrl Pts',(16.6717400398738,-18.4736629064988,
3.93794331645963));
#171891=CARTESIAN_POINT('Ctrl Pts',(16.6704395973768,-18.4793045539916,
3.93759611096546));
#171892=CARTESIAN_POINT('Ctrl Pts',(16.6657019231395,-18.5002499787928,
3.9363129626332));
#171893=CARTESIAN_POINT('Ctrl Pts',(16.6624115605977,-18.5155869082596,
3.93538506602472));
#171894=CARTESIAN_POINT('Ctrl Pts',(16.632554547465,-18.6627095418791,3.92658315316966));
#171895=CARTESIAN_POINT('Ctrl Pts',(16.6184239853392,-18.7967259490059,
3.91931202279268));
#171896=CARTESIAN_POINT('Ctrl Pts',(16.6170404625804,-18.9374793398567,
3.91166809579151));
#171897=CARTESIAN_POINT('Ctrl Pts',(16.6170066729722,-18.94376677829,3.91132666064666));
#171898=CARTESIAN_POINT('Ctrl Pts',(16.6168668544331,-19.0958927648747,
3.90306443006442));
#171899=CARTESIAN_POINT('Ctrl Pts',(16.6318021047659,-19.2413359707292,
3.89510371418586));
#171900=CARTESIAN_POINT('Ctrl Pts',(16.6664676942097,-19.4076057064771,
3.88524445554732));
#171901=CARTESIAN_POINT('Ctrl Pts',(16.6717720440742,-19.4310429873341,
3.88383767302017));
#171902=CARTESIAN_POINT('Ctrl Pts',(16.6797804435962,-19.4638256282852,
3.88184394360458));
#171903=CARTESIAN_POINT('Ctrl Pts',(16.6821518237267,-19.4732509150305,
3.88126769147224));
#171904=CARTESIAN_POINT('Ctrl Pts',(16.6860916184719,-19.4884664418707,
3.88033238345868));
#171905=CARTESIAN_POINT('Ctrl Pts',(16.6876199075509,-19.4942669992487,
3.87997462882876));
#171906=CARTESIAN_POINT('Ctrl Pts',(16.690855325819,-19.5063384146194,3.87922759582056));
#171907=CARTESIAN_POINT('Ctrl Pts',(16.6925667182077,-19.5126080556736,
3.87883818238362));
#171908=CARTESIAN_POINT('Ctrl Pts',(16.696678362728,-19.5274024490659,3.87791588445684));
#171909=CARTESIAN_POINT('Ctrl Pts',(16.6991032784907,-19.5359201667639,
3.87738220201063));
#171910=CARTESIAN_POINT('Ctrl Pts',(16.7073169381373,-19.5640987025324,
3.87560762706832));
#171911=CARTESIAN_POINT('Ctrl Pts',(16.7133376061603,-19.5836901919816,
3.87435919381296));
#171912=CARTESIAN_POINT('Ctrl Pts',(16.7467230010809,-19.6869627894031,
3.86769849643721));
#171913=CARTESIAN_POINT('Ctrl Pts',(16.779000315155,-19.7689534976003,3.86212557703156));
#171914=CARTESIAN_POINT('Ctrl Pts',(16.8711049179755,-19.965934299276,3.84804780837658));
#171915=CARTESIAN_POINT('Ctrl Pts',(16.9365619694566,-20.077901295827,3.8394138807018));
#171916=CARTESIAN_POINT('Ctrl Pts',(17.0275742721489,-20.2052093000958,
3.82914899890504));
#171917=CARTESIAN_POINT('Ctrl Pts',(17.0437446644012,-20.2269350140777,
3.82738096877477));
#171918=CARTESIAN_POINT('Ctrl Pts',(17.0955034772297,-20.2937592648694,
3.82190413977418));
#171919=CARTESIAN_POINT('Ctrl Pts',(17.1325165343988,-20.3377275162307,
3.81824355734129));
#171920=CARTESIAN_POINT('Ctrl Pts',(17.177263699391,-20.3866915617919,3.81415056233225));
#171921=CARTESIAN_POINT('Ctrl Pts',(17.1832929079751,-20.3932061990514,
3.81360565013237));
#171922=CARTESIAN_POINT('Ctrl Pts',(17.1924516927485,-20.4029783653255,
3.81278801143652));
#171923=CARTESIAN_POINT('Ctrl Pts',(17.1955509247917,-20.4062640214547,
3.81251305647396));
#171924=CARTESIAN_POINT('Ctrl Pts',(17.2011160478794,-20.412126195834,3.81202245328679));
#171925=CARTESIAN_POINT('Ctrl Pts',(17.2035779471775,-20.4147064159544,
3.81180650539683));
#171926=CARTESIAN_POINT('Ctrl Pts',(17.2089220783741,-20.4202791268719,
3.81134008865029));
#171927=CARTESIAN_POINT('Ctrl Pts',(17.2118065936837,-20.4232693485176,
3.81108980172376));
#171928=CARTESIAN_POINT('Ctrl Pts',(17.219884606349,-20.4315942026561,3.81039288602945));
#171929=CARTESIAN_POINT('Ctrl Pts',(17.2250975285736,-20.4369100192551,
3.80994774472222));
#171930=CARTESIAN_POINT('Ctrl Pts',(17.2554562683131,-20.4675430353591,
3.80738102866061));
#171931=CARTESIAN_POINT('Ctrl Pts',(17.281212535892,-20.4922503634395,3.80530467626046));
#171932=CARTESIAN_POINT('Ctrl Pts',(17.3658586632785,-20.5694356715784,
3.79874973221874));
#171933=CARTESIAN_POINT('Ctrl Pts',(17.4270632496412,-20.6192813612031,
3.79440821669894));
#171934=CARTESIAN_POINT('Ctrl Pts',(17.5646408986174,-20.7190837759748,
3.78513876655965));
#171935=CARTESIAN_POINT('Ctrl Pts',(17.641744789346,-20.7677544465143,3.78023182358685));
#171936=CARTESIAN_POINT('Ctrl Pts',(17.8150630554438,-20.86211352856,3.76938613693422));
#171937=CARTESIAN_POINT('Ctrl Pts',(17.9120634607094,-20.9058154646793,
3.76342351390248));
#171938=CARTESIAN_POINT('Ctrl Pts',(18.0251856585078,-20.9468609432434,
3.75637196410921));
#171939=CARTESIAN_POINT('Ctrl Pts',(18.038492413508,-20.951539231015,3.7555411909062));
#171940=CARTESIAN_POINT('Ctrl Pts',(18.0597976158504,-20.9587911506411,
3.75420858579345));
#171941=CARTESIAN_POINT('Ctrl Pts',(18.0677664960331,-20.9614507936679,
3.75370959922164));
#171942=CARTESIAN_POINT('Ctrl Pts',(18.0818794258604,-20.9660678576787,
3.75282484182403));
#171943=CARTESIAN_POINT('Ctrl Pts',(18.0880170176879,-20.9680447821648,
3.75243971942586));
#171944=CARTESIAN_POINT('Ctrl Pts',(18.1007603097913,-20.9720852426614,
3.75163933827889));
#171945=CARTESIAN_POINT('Ctrl Pts',(18.1073672806373,-20.9741444869565,
3.75122394384581));
#171946=CARTESIAN_POINT('Ctrl Pts',(18.1244160986399,-20.9793666423947,
3.75015090195569));
#171947=CARTESIAN_POINT('Ctrl Pts',(18.1348724171269,-20.9824812651078,
3.74949168306891));
#171948=CARTESIAN_POINT('Ctrl Pts',(18.179165365773,-20.9953028811977,3.74669426657776));
#171949=CARTESIAN_POINT('Ctrl Pts',(18.2132156897672,-21.0042455029274,
3.74453140916394));
#171950=CARTESIAN_POINT('Ctrl Pts',(18.3030452731752,-21.0254579030511,
3.73878992001805));
#171951=CARTESIAN_POINT('Ctrl Pts',(18.359122873625,-21.0363262425726,3.73516960252828));
#171952=CARTESIAN_POINT('Ctrl Pts',(18.5659612572872,-21.067796271307,3.72170022785271));
#171953=CARTESIAN_POINT('Ctrl Pts',(18.7183789724776,-21.0743996040648,
3.71151257409928));
#171954=CARTESIAN_POINT('Ctrl Pts',(18.8926143489366,-21.0631694621775,
3.70010873248781));
#171955=CARTESIAN_POINT('Ctrl Pts',(18.915038513217,-21.0613648609432,3.69864662224109));
#171956=CARTESIAN_POINT('Ctrl Pts',(18.9885573577788,-21.0542673241109,
3.6938793084805));
#171957=CARTESIAN_POINT('Ctrl Pts',(19.0394927019095,-21.0474719031565,
3.6906179728685));
#171958=CARTESIAN_POINT('Ctrl Pts',(19.0978982595057,-21.0375045163014,
3.68696358198722));
#171959=CARTESIAN_POINT('Ctrl Pts',(19.1056546613206,-21.0361362354488,
3.6864800244708));
#171960=CARTESIAN_POINT('Ctrl Pts',(19.1180095511047,-21.0338855841562,
3.68571277998383));
#171961=CARTESIAN_POINT('Ctrl Pts',(19.1226129739211,-21.0330312055151,
3.6854275700628));
#171962=CARTESIAN_POINT('Ctrl Pts',(19.1307440240269,-21.0314941906244,
3.68492502409105));
#171963=CARTESIAN_POINT('Ctrl Pts',(19.134272795892,-21.0308178369106,3.68470733437687));
#171964=CARTESIAN_POINT('Ctrl Pts',(19.1417296701644,-21.0293688989211,
3.68424819967114));
#171965=CARTESIAN_POINT('Ctrl Pts',(19.1456573008308,-21.0285941571289,
3.68400687929838));
#171966=CARTESIAN_POINT('Ctrl Pts',(19.1562102240672,-21.0264814317415,
3.68335980871724));
#171967=CARTESIAN_POINT('Ctrl Pts',(19.162831410307,-21.0251228396548,3.68295521881514));
#171968=CARTESIAN_POINT('Ctrl Pts',(19.1951348592948,-21.0183331552229,
3.6809876451806));
#171969=CARTESIAN_POINT('Ctrl Pts',(19.2207223335718,-21.0124561581417,
3.67944873086008));
#171970=CARTESIAN_POINT('Ctrl Pts',(19.2937036806347,-20.9942581091047,
3.6750985937067));
#171971=CARTESIAN_POINT('Ctrl Pts',(19.3407901344176,-20.9807663142388,
3.67233961646863));
#171972=CARTESIAN_POINT('Ctrl Pts',(19.4792756662508,-20.9358319654717,
3.66425591350563));
#171973=CARTESIAN_POINT('Ctrl Pts',(19.5690360765545,-20.8997528818413,
3.65905285182928));
#171974=CARTESIAN_POINT('Ctrl Pts',(19.7829857781843,-20.7962373969938,
3.64611983252081));
#171975=CARTESIAN_POINT('Ctrl Pts',(19.9034758404611,-20.7222828772199,
3.63834011682043));
#171976=CARTESIAN_POINT('Ctrl Pts',(20.0270790917159,-20.6282575770136,
3.62924195725224));
#171977=CARTESIAN_POINT('Ctrl Pts',(20.0383587492272,-20.6194954993507,
3.62840085445846));
#171978=CARTESIAN_POINT('Ctrl Pts',(20.0561711612286,-20.6053674329431,
3.62705480177545));
#171979=CARTESIAN_POINT('Ctrl Pts',(20.0627620503884,-20.6000751979773,
3.62655278944008));
#171980=CARTESIAN_POINT('Ctrl Pts',(20.0743310926665,-20.5906711837373,
3.62566451474313));
#171981=CARTESIAN_POINT('Ctrl Pts',(20.0793224881636,-20.5865758128014,
3.6252789177452));
#171982=CARTESIAN_POINT('Ctrl Pts',(20.089608460664,-20.5780572860882,3.62447936951975));
#171983=CARTESIAN_POINT('Ctrl Pts',(20.0949003005306,-20.5736309587965,
3.62406529158296));
#171984=CARTESIAN_POINT('Ctrl Pts',(20.1084301930492,-20.5622010926669,
3.62299949835742));
#171985=CARTESIAN_POINT('Ctrl Pts',(20.1166363212192,-20.5551602261918,
3.62234625199899));
#171986=CARTESIAN_POINT('Ctrl Pts',(20.1506782839383,-20.5254964001308,
3.61960737641389));
#171987=CARTESIAN_POINT('Ctrl Pts',(20.1760144769206,-20.5023103924026,
3.61749835576717));
#171988=CARTESIAN_POINT('Ctrl Pts',(20.2405660387311,-20.440285253731,3.61193376400569));
#171989=CARTESIAN_POINT('Ctrl Pts',(20.2788444740461,-20.4005126690312,
3.60843963293878));
#171990=CARTESIAN_POINT('Ctrl Pts',(20.388288080156,-20.2775193627391,3.59785656492648));
#171991=CARTESIAN_POINT('Ctrl Pts',(20.4545961724365,-20.1902309883408,
3.59061928252106));
#171992=CARTESIAN_POINT('Ctrl Pts',(20.5427363516408,-20.0533662161876,
3.57986596111988));
#171993=CARTESIAN_POINT('Ctrl Pts',(20.5699147097805,-20.0074393632676,
3.57634996540707));
#171994=CARTESIAN_POINT('Ctrl Pts',(20.6013704200902,-19.9493853261275,
3.57205283183505));
#171995=CARTESIAN_POINT('Ctrl Pts',(20.6073108039685,-19.9381827496778,
3.57123023453653));
#171996=CARTESIAN_POINT('Ctrl Pts',(20.6376760878161,-19.8796543547082,
3.56696904540654));
#171997=CARTESIAN_POINT('Ctrl Pts',(20.6604116623662,-19.8314682417883,
3.56358373409534));
#171998=CARTESIAN_POINT('Ctrl Pts',(20.6847259255766,-19.7744556574431,
3.55976032947201));
#171999=CARTESIAN_POINT('Ctrl Pts',(20.6880951091711,-19.7664183540963,
3.55922545513258));
#172000=CARTESIAN_POINT('Ctrl Pts',(20.6931218175638,-19.7542161755697,
3.55841989885514));
#172001=CARTESIAN_POINT('Ctrl Pts',(20.6948158573049,-19.7500665780477,
3.55814708319013));
#172002=CARTESIAN_POINT('Ctrl Pts',(20.6978332232313,-19.7426078498529,
3.55765877552597));
#172003=CARTESIAN_POINT('Ctrl Pts',(20.6991613773727,-19.7393007445581,
3.55744299578883));
#172004=CARTESIAN_POINT('Ctrl Pts',(20.7020294311448,-19.7321068106624,
3.55697519917203));
#172005=CARTESIAN_POINT('Ctrl Pts',(20.7035661655875,-19.7282187822778,
3.55672337361937));
#172006=CARTESIAN_POINT('Ctrl Pts',(20.7078510426248,-19.7172831383104,
3.556017814126));
#172007=CARTESIAN_POINT('Ctrl Pts',(20.710572975948,-19.7102252270398,3.5555656280204));
#172008=CARTESIAN_POINT('Ctrl Pts',(20.7266319304302,-19.6679105329622,
3.55287276722474));
#172009=CARTESIAN_POINT('Ctrl Pts',(20.7390640788338,-19.6323148805782,
3.55068267056642));
#172010=CARTESIAN_POINT('Ctrl Pts',(20.7768715595335,-19.5140035235451,
3.54359032882097));
#172011=CARTESIAN_POINT('Ctrl Pts',(20.7981301497969,-19.4300598925435,
3.53885232704573));
#172012=CARTESIAN_POINT('Ctrl Pts',(20.8469054621098,-19.1719163043558,
3.52455637502355));
#172013=CARTESIAN_POINT('Ctrl Pts',(20.8578743442905,-18.9954024848503,
3.51508742487422));
#172014=CARTESIAN_POINT('Ctrl Pts',(20.8454190730435,-18.7966784798802,
3.50351662147154));
#172015=CARTESIAN_POINT('Ctrl Pts',(20.8436120272572,-18.7738082197345,
3.50217258131649));
#172016=CARTESIAN_POINT('Ctrl Pts',(20.8405280284339,-18.7414777056704,
3.50025325244852));
#172017=CARTESIAN_POINT('Ctrl Pts',(20.8395581804588,-18.7319892839764,
3.49968760404709));
#172018=CARTESIAN_POINT('Ctrl Pts',(20.8378775880425,-18.716577656134,3.49876488897144));
#172019=CARTESIAN_POINT('Ctrl Pts',(20.8372058598235,-18.7106502630181,
3.49840905502558));
#172020=CARTESIAN_POINT('Ctrl Pts',(20.8357468337911,-18.6982445371956,
3.49766228331828));
#172021=CARTESIAN_POINT('Ctrl Pts',(20.8349546158209,-18.6917668563875,
3.49727119388797));
#172022=CARTESIAN_POINT('Ctrl Pts',(20.8329976936481,-18.6763574529723,
3.49633804291479));
#172023=CARTESIAN_POINT('Ctrl Pts',(20.8318059189893,-18.6674293514684,
3.49579513140122));
#172024=CARTESIAN_POINT('Ctrl Pts',(20.8275936394899,-18.6373388477539,
3.49395760483708));
#172025=CARTESIAN_POINT('Ctrl Pts',(20.8243096625917,-18.6162152029563,
3.49265469530736));
#172026=CARTESIAN_POINT('Ctrl Pts',(20.8046466900077,-18.5012359833599,
3.48548961692087));
#172027=CARTESIAN_POINT('Ctrl Pts',(20.7822681291721,-18.4085302677464,
3.47943826093059));
#172028=CARTESIAN_POINT('Ctrl Pts',(20.7026061183242,-18.1548893669231,
3.46216230876742));
#172029=CARTESIAN_POINT('Ctrl Pts',(20.6320015056481,-17.9989089470511,
3.4506509601528));
#172030=CARTESIAN_POINT('Ctrl Pts',(20.5243810106594,-17.8217018303696,
3.43741904338694));
#172031=CARTESIAN_POINT('Ctrl Pts',(20.5044996556448,-17.7908068806401,
3.43510868194865));
#172032=CARTESIAN_POINT('Ctrl Pts',(20.4798052598489,-17.754542714772,3.43240694704327));
#172033=CARTESIAN_POINT('Ctrl Pts',(20.4757575757676,-17.7486627630497,
3.43196921080564));
#172034=CARTESIAN_POINT('Ctrl Pts',(20.4691034195864,-17.7391003856303,
3.43125802286862));
#172035=CARTESIAN_POINT('Ctrl Pts',(20.4665148194733,-17.7354056746906,
3.43098340320532));
#172036=CARTESIAN_POINT('Ctrl Pts',(20.4618589570356,-17.7288053547797,
3.43049316130316));
#172037=CARTESIAN_POINT('Ctrl Pts',(20.4597961532816,-17.7258966791383,
3.43027724126631));
#172038=CARTESIAN_POINT('Ctrl Pts',(20.4553116804107,-17.7196070458605,
3.42981061508776));
#172039=CARTESIAN_POINT('Ctrl Pts',(20.4528874030935,-17.7162280183219,
3.42956009232295));
#172040=CARTESIAN_POINT('Ctrl Pts',(20.4460846258646,-17.7068048603717,
3.42886185382716));
#172041=CARTESIAN_POINT('Ctrl Pts',(20.4416840478306,-17.700776639275,3.42841563472515));
#172042=CARTESIAN_POINT('Ctrl Pts',(20.4158828933032,-17.6658220821281,
3.42583012754213));
#172043=CARTESIAN_POINT('Ctrl Pts',(20.3937781263936,-17.6374199827396,
3.42373683954992));
#172044=CARTESIAN_POINT('Ctrl Pts',(20.3202496593505,-17.5477578381783,
3.41710375865058));
#172045=CARTESIAN_POINT('Ctrl Pts',(20.2660735486265,-17.488840176102,3.41270483440733));
#172046=CARTESIAN_POINT('Ctrl Pts',(20.0753509676859,-17.3036658052757,
3.39821265384092));
#172047=CARTESIAN_POINT('Ctrl Pts',(19.9255630372144,-17.1923410637516,
3.38827387289251));
#172048=CARTESIAN_POINT('Ctrl Pts',(19.7438713173816,-17.0912644980932,
3.37618125019198));
#172049=CARTESIAN_POINT('Ctrl Pts',(19.7244066973028,-17.080831593482,3.37488667870934));
#172050=CARTESIAN_POINT('Ctrl Pts',(19.6972690732012,-17.0668280756215,
3.37308152395338));
#172051=CARTESIAN_POINT('Ctrl Pts',(19.689732116709,-17.0629958682443,3.37258015212272));
#172052=CARTESIAN_POINT('Ctrl Pts',(19.6767390402116,-17.0564871320048,
3.37171569961167));
#172053=CARTESIAN_POINT('Ctrl Pts',(19.6712939426879,-17.0537887381825,
3.37135338879623));
#172054=CARTESIAN_POINT('Ctrl Pts',(19.660046122388,-17.0482749208505,3.37060485610026));
#172055=CARTESIAN_POINT('Ctrl Pts',(19.6542420064951,-17.045462498185,3.37021853444855));
#172056=CARTESIAN_POINT('Ctrl Pts',(19.6407080021807,-17.03898070744,3.36931752284501));
#172057=CARTESIAN_POINT('Ctrl Pts',(19.6329685791368,-17.035331613113,3.36880213631401));
#172058=CARTESIAN_POINT('Ctrl Pts',(19.6081365252051,-17.0238069297383,
3.36714793310628));
#172059=CARTESIAN_POINT('Ctrl Pts',(19.590961280438,-17.0161124751592,3.36600291251167));
#172060=CARTESIAN_POINT('Ctrl Pts',(19.5047183302013,-16.9788485005279,
3.36024747716289));
#172061=CARTESIAN_POINT('Ctrl Pts',(19.434220581151,-16.9527444962991,3.35552131377385));
#172062=CARTESIAN_POINT('Ctrl Pts',(19.2583709749715,-16.8980737815082,
3.3436886695316));
#172063=CARTESIAN_POINT('Ctrl Pts',(19.1519128260614,-16.8737980788603,
3.33648210440557));
#172064=CARTESIAN_POINT('Ctrl Pts',(18.9258875206594,-16.8403321465337,
3.32138759652239));
#172065=CARTESIAN_POINT('Ctrl Pts',(18.8064229707569,-16.8328672804233,
3.31352759279534));
#172066=CARTESIAN_POINT('Ctrl Pts',(18.6774513080357,-16.8357340392992,
3.30555982556304));
#172067=CARTESIAN_POINT('Ctrl Pts',(18.6679486157786,-16.8360093116053,
3.30497586470134));
#172068=CARTESIAN_POINT('Ctrl Pts',(18.6538681276579,-16.8365121404063,
3.30411551617469));
#172069=CARTESIAN_POINT('Ctrl Pts',(18.649288849566,-16.8366905609444,3.30383648511564));
#172070=CARTESIAN_POINT('Ctrl Pts',(18.6411413416848,-16.8370345088922,
3.30334144855333));
#172071=CARTESIAN_POINT('Ctrl Pts',(18.6375729229334,-16.8371941984035,
3.30312512073868));
#172072=CARTESIAN_POINT('Ctrl Pts',(18.6299006553742,-16.8375569980548,
3.30266106082491));
#172073=CARTESIAN_POINT('Ctrl Pts',(18.6257970007285,-16.8377630233025,
3.30241349378027));
#172074=CARTESIAN_POINT('Ctrl Pts',(18.6144685825303,-16.8383648391347,
3.30173178280331));
#172075=CARTESIAN_POINT('Ctrl Pts',(18.6072451298914,-16.8387857280082,
3.30129902277524));
#172076=CARTESIAN_POINT('Ctrl Pts',(18.5676406782732,-16.8412971636477,
3.29893618019018));
#172077=CARTESIAN_POINT('Ctrl Pts',(18.5353069688865,-16.8440950622238,
3.29704333166913));
#172078=CARTESIAN_POINT('Ctrl Pts',(18.3412644645688,-16.8653910016222,
3.28583412540617));
#172079=CARTESIAN_POINT('Ctrl Pts',(18.1820510116922,-16.9017457470014,
3.27723163670283));
#172080=CARTESIAN_POINT('Ctrl Pts',(17.9183983242485,-16.9949269006738,
3.26192319637002));
#172081=CARTESIAN_POINT('Ctrl Pts',(17.8116605124413,-17.0429096882309,
3.25540051232392));
#172082=CARTESIAN_POINT('Ctrl Pts',(17.6958125176361,-17.10698021256,3.24764506512588));
#172083=CARTESIAN_POINT('Ctrl Pts',(17.6822757385203,-17.1146629805324,
3.24672806874611));
#172084=CARTESIAN_POINT('Ctrl Pts',(17.6618266740128,-17.1265688342497,
3.24532580519973));
#172085=CARTESIAN_POINT('Ctrl Pts',(17.654851690941,-17.1306835788032,3.24484445694518));
#172086=CARTESIAN_POINT('Ctrl Pts',(17.6425600849073,-17.138030148823,3.24399071904006));
#172087=CARTESIAN_POINT('Ctrl Pts',(17.6372337498715,-17.1412455990557,
3.24361893042769));
#172088=CARTESIAN_POINT('Ctrl Pts',(17.6259970729934,-17.1480968251368,
3.24283065437021));
#172089=CARTESIAN_POINT('Ctrl Pts',(17.6200902883704,-17.1517382681706,
3.2424139615277));
#172090=CARTESIAN_POINT('Ctrl Pts',(17.6080390813448,-17.1592496717812,
3.24155900558252));
#172091=CARTESIAN_POINT('Ctrl Pts',(17.6018964596143,-17.1631223346866,
3.24112064608034));
#172092=CARTESIAN_POINT('Ctrl Pts',(17.586754859295,-17.1727776958993,3.24003363226849));
#172093=CARTESIAN_POINT('Ctrl Pts',(17.5777796275607,-17.1785970948363,
3.23938361821268));
#172094=CARTESIAN_POINT('Ctrl Pts',(17.4712655729678,-17.2488114344553,
3.23160074071753));
#172095=CARTESIAN_POINT('Ctrl Pts',(17.3791929616813,-17.3210985407488,
3.22416359540188));
#172096=CARTESIAN_POINT('Ctrl Pts',(17.1575742715224,-17.5268658373759,
3.20441839977583));
#172097=CARTESIAN_POINT('Ctrl Pts',(17.0387764816844,-17.6704600483137,
3.19185515152312));
#172098=CARTESIAN_POINT('Ctrl Pts',(16.9326610880885,-17.839763629678,3.17941612942038));
#172099=CARTESIAN_POINT('Ctrl Pts',(16.9252230606113,-17.8519010827888,
3.17853668626084));
#172100=CARTESIAN_POINT('Ctrl Pts',(16.9150488886815,-17.8688855990024,
3.17732406635359));
#172101=CARTESIAN_POINT('Ctrl Pts',(16.9122087663511,-17.8736695063082,
3.17698448413844));
#172102=CARTESIAN_POINT('Ctrl Pts',(16.9076800568673,-17.8813666349358,
3.17644133050573));
#172103=CARTESIAN_POINT('Ctrl Pts',(16.9059795267723,-17.8842727469519,
3.17623699190379));
#172104=CARTESIAN_POINT('Ctrl Pts',(16.9024417716782,-17.8903518007728,
3.17581110315119));
#172105=CARTESIAN_POINT('Ctrl Pts',(16.9006058499074,-17.8935254687615,
3.1755896421561));
#172106=CARTESIAN_POINT('Ctrl Pts',(16.8961844996462,-17.901214456298,3.17505518944349));
#172107=CARTESIAN_POINT('Ctrl Pts',(16.8936074330109,-17.9057346068626,
3.17474273630196));
#172108=CARTESIAN_POINT('Ctrl Pts',(16.8846505067469,-17.9215804623655,
3.1736533007204));
#172109=CARTESIAN_POINT('Ctrl Pts',(16.8783581697579,-17.9329556493819,
3.17288173911637));
#172110=CARTESIAN_POINT('Ctrl Pts',(16.841827006579,-18.0004566431848,3.16836065650515));
#172111=CARTESIAN_POINT('Ctrl Pts',(16.8140283819398,-18.0578725289664,
3.16474736288815));
#172112=CARTESIAN_POINT('Ctrl Pts',(16.7733550786844,-18.1525601282371,
3.1590194040154));
#172113=CARTESIAN_POINT('Ctrl Pts',(16.7588705942293,-18.1890512064045,
3.15686514330449));
#172114=CARTESIAN_POINT('Ctrl Pts',(16.7454192974521,-18.225889960506,3.15472450021249));
#172115=CARTESIAN_POINT('Ctrl Pts',(16.7454193844899,-18.2258897221376,
2.93545674301194));
#172116=CARTESIAN_POINT('Ctrl Pts',(16.7759470815439,-18.1422842582728,
2.94055495122605));
#172117=CARTESIAN_POINT('Ctrl Pts',(16.8117309549823,-18.0606488015625,
2.94543447229376));
#172118=CARTESIAN_POINT('Ctrl Pts',(16.8782378463899,-17.931720516084,2.95332993456547));
#172119=CARTESIAN_POINT('Ctrl Pts',(16.9058676585179,-17.8830025582496,
2.95636023097386));
#172120=CARTESIAN_POINT('Ctrl Pts',(16.9829403244133,-17.7588508291059,
2.96432632192045));
#172121=CARTESIAN_POINT('Ctrl Pts',(17.0353246888041,-17.6853843571324,
2.96929182853531));
#172122=CARTESIAN_POINT('Ctrl Pts',(17.1225828220143,-17.5781967170225,
2.97715510187905));
#172123=CARTESIAN_POINT('Ctrl Pts',(17.1541971425227,-17.5419563147247,
2.97993326331005));
#172124=CARTESIAN_POINT('Ctrl Pts',(17.1951439827439,-17.4981248607339,
2.98346365873175));
#172125=CARTESIAN_POINT('Ctrl Pts',(17.203345040904,-17.4894931966346,2.98416750350011));
#172126=CARTESIAN_POINT('Ctrl Pts',(17.2166778947079,-17.4756952740827,
2.98530684168578));
#172127=CARTESIAN_POINT('Ctrl Pts',(17.221764368589,-17.4704854344176,2.98574036242394));
#172128=CARTESIAN_POINT('Ctrl Pts',(17.2313501507484,-17.4607679617444,
2.98655529820242));
#172129=CARTESIAN_POINT('Ctrl Pts',(17.2358431310879,-17.4562541806395,
2.98693643215704));
#172130=CARTESIAN_POINT('Ctrl Pts',(17.2459428252301,-17.4461988883982,
2.98779135310418));
#172131=CARTESIAN_POINT('Ctrl Pts',(17.2515602398015,-17.4406683031692,
2.98826561433618));
#172132=CARTESIAN_POINT('Ctrl Pts',(17.2658704372284,-17.4267358453692,
2.98947072735871));
#172133=CARTESIAN_POINT('Ctrl Pts',(17.2746044567646,-17.418376906356,2.99020343246399));
#172134=CARTESIAN_POINT('Ctrl Pts',(17.3248503942984,-17.3711066757997,
2.99440318358987));
#172135=CARTESIAN_POINT('Ctrl Pts',(17.3678427366168,-17.3338097525053,
2.99793819039885));
#172136=CARTESIAN_POINT('Ctrl Pts',(17.4333458490969,-17.2814567054356,
3.00324450435915));
#172137=CARTESIAN_POINT('Ctrl Pts',(17.4547288890248,-17.2650259476538,
3.00496480060166));
#172138=CARTESIAN_POINT('Ctrl Pts',(17.6003778284853,-17.1574709138737,
3.01659910237716));
#172139=CARTESIAN_POINT('Ctrl Pts',(17.7339561624323,-17.0797450510681,
3.02691629130477));
#172140=CARTESIAN_POINT('Ctrl Pts',(17.9219735294178,-16.9962468782493,
3.04036301841443));
#172141=CARTESIAN_POINT('Ctrl Pts',(17.9699375952316,-16.977014779409,3.04370271288394));
#172142=CARTESIAN_POINT('Ctrl Pts',(18.0441765915031,-16.9503573062147,
3.04868882247872));
#172143=CARTESIAN_POINT('Ctrl Pts',(18.0699694517278,-16.9416534124646,
3.05038822796867));
#172144=CARTESIAN_POINT('Ctrl Pts',(18.1024471678401,-16.9313870190893,
3.05248095324582));
#172145=CARTESIAN_POINT('Ctrl Pts',(18.108980034542,-16.9293567185075,3.05289953840353));
#172146=CARTESIAN_POINT('Ctrl Pts',(18.1193687795427,-16.9261832177474,
3.05356130598534));
#172147=CARTESIAN_POINT('Ctrl Pts',(18.1232182057589,-16.9250192963761,
3.05380567339267));
#172148=CARTESIAN_POINT('Ctrl Pts',(18.1305088015917,-16.9228375494816,
3.05426686675133));
#172149=CARTESIAN_POINT('Ctrl Pts',(18.1339491990775,-16.9218175171612,
3.0544838147274));
#172150=CARTESIAN_POINT('Ctrl Pts',(18.1418526035801,-16.9194961077351,
3.05498064246653));
#172151=CARTESIAN_POINT('Ctrl Pts',(18.1463173115717,-16.9182006810346,
3.05526017331096));
#172152=CARTESIAN_POINT('Ctrl Pts',(18.1582482856154,-16.9147814997828,
3.0560042297709));
#172153=CARTESIAN_POINT('Ctrl Pts',(18.1657221063818,-16.9126840622291,
3.056467266286));
#172154=CARTESIAN_POINT('Ctrl Pts',(18.2200966986481,-16.8977466260996,
3.05981497436556));
#172155=CARTESIAN_POINT('Ctrl Pts',(18.2674198841836,-16.886483765382,3.0626151490539));
#172156=CARTESIAN_POINT('Ctrl Pts',(18.3418054726836,-16.8714675922194,
3.0669002103813));
#172157=CARTESIAN_POINT('Ctrl Pts',(18.3686206275118,-16.8665912509613,
3.06842165420803));
#172158=CARTESIAN_POINT('Ctrl Pts',(18.5444152053767,-16.8381180255152,
3.07828623215645));
#172159=CARTESIAN_POINT('Ctrl Pts',(18.6954586479851,-16.8299828652455,
3.08628188131668));
#172160=CARTESIAN_POINT('Ctrl Pts',(18.9027629555578,-16.8409744005262,
3.09780984267062));
#172161=CARTESIAN_POINT('Ctrl Pts',(18.9592900578601,-16.84625696929,3.10100617960215));
#172162=CARTESIAN_POINT('Ctrl Pts',(19.0502689829886,-16.8584644307665,
3.10628390994597));
#172163=CARTESIAN_POINT('Ctrl Pts',(19.0848813825118,-16.8639867587772,
3.10832317482897));
#172164=CARTESIAN_POINT('Ctrl Pts',(19.1300503338849,-16.8723481567688,
3.11103198762125));
#172165=CARTESIAN_POINT('Ctrl Pts',(19.1407456792376,-16.8744135152211,
3.11167690606008));
#172166=CARTESIAN_POINT('Ctrl Pts',(19.1582053094646,-16.8779250989166,
3.11273563594417));
#172167=CARTESIAN_POINT('Ctrl Pts',(19.1649793716629,-16.8793221139459,
3.1131478713426));
#172168=CARTESIAN_POINT('Ctrl Pts',(19.1780566089302,-16.8820859135468,
3.11394656887917));
#172169=CARTESIAN_POINT('Ctrl Pts',(19.1843606305514,-16.8834483573636,
3.11433288789866));
#172170=CARTESIAN_POINT('Ctrl Pts',(19.1988703577518,-16.8866537142894,
3.1152251007538));
#172171=CARTESIAN_POINT('Ctrl Pts',(19.2070714636147,-16.8885167515727,
3.11573163611591));
#172172=CARTESIAN_POINT('Ctrl Pts',(19.2290272643409,-16.8936421981323,
3.11709384074838));
#172173=CARTESIAN_POINT('Ctrl Pts',(19.2427605651743,-16.8969935510907,
3.1179523583835));
#172174=CARTESIAN_POINT('Ctrl Pts',(19.3609862861363,-16.9271020355118,
3.12540014510187));
#172175=CARTESIAN_POINT('Ctrl Pts',(19.4633101018816,-16.9616673310542,
3.13224467165334));
#172176=CARTESIAN_POINT('Ctrl Pts',(19.682284609536,-17.0547976318088,3.14773322831267));
#172177=CARTESIAN_POINT('Ctrl Pts',(19.7970691509984,-17.1166520128045,
3.15643004234202));
#172178=CARTESIAN_POINT('Ctrl Pts',(19.9461973452119,-17.2157223211458,
3.16811289623007));
#172179=CARTESIAN_POINT('Ctrl Pts',(19.9860007734155,-17.2442010430706,
3.17127003906701));
#172180=CARTESIAN_POINT('Ctrl Pts',(20.0455788678032,-17.2900318314815,
3.17601653352989));
#172181=CARTESIAN_POINT('Ctrl Pts',(20.0660757446133,-17.3064144881906,
3.17765342343682));
#172182=CARTESIAN_POINT('Ctrl Pts',(20.091463258744,-17.327491407066,3.17968031742504));
#172183=CARTESIAN_POINT('Ctrl Pts',(20.096642081454,-17.3318329629149,3.18009375407533));
#172184=CARTESIAN_POINT('Ctrl Pts',(20.1048553908031,-17.3387856554528,
3.18074926601894));
#172185=CARTESIAN_POINT('Ctrl Pts',(20.1079033629727,-17.3413806862658,
3.18099248895619));
#172186=CARTESIAN_POINT('Ctrl Pts',(20.1136732040162,-17.3463214018786,
3.18145280795395));
#172187=CARTESIAN_POINT('Ctrl Pts',(20.116396427197,-17.3486653410558,3.18167001884687));
#172188=CARTESIAN_POINT('Ctrl Pts',(20.1226548573037,-17.3540799103537,
3.18216911898711));
#172189=CARTESIAN_POINT('Ctrl Pts',(20.1261858521274,-17.3571553430793,
3.18245064823499));
#172190=CARTESIAN_POINT('Ctrl Pts',(20.1356298441975,-17.3654361537914,
3.18320355028272));
#172191=CARTESIAN_POINT('Ctrl Pts',(20.1415241038807,-17.3706629203105,
3.18367337757931));
#172192=CARTESIAN_POINT('Ctrl Pts',(20.185662776115,-17.4102454426791,3.1871922595319));
#172193=CARTESIAN_POINT('Ctrl Pts',(20.2226768681572,-17.4459541722953,
3.19014678140815));
#172194=CARTESIAN_POINT('Ctrl Pts',(20.2681769694972,-17.4931681752255,
3.19384034453995));
#172195=CARTESIAN_POINT('Ctrl Pts',(20.2778947156805,-17.5034564602049,
3.19463299310619));
#172196=CARTESIAN_POINT('Ctrl Pts',(20.3959786432631,-17.6310115394064,
3.20432288012174));
#172197=CARTESIAN_POINT('Ctrl Pts',(20.490847236747,-17.760078821804,3.21275663181213));
#172198=CARTESIAN_POINT('Ctrl Pts',(20.5989632037442,-17.9485469210057,
3.2248143437229));
#172199=CARTESIAN_POINT('Ctrl Pts',(20.6255684271208,-17.9996481757029,
3.22805588697978));
#172200=CARTESIAN_POINT('Ctrl Pts',(20.6651178004025,-18.0838251539264,
3.23340152458345));
#172201=CARTESIAN_POINT('Ctrl Pts',(20.6793718703327,-18.1162538705707,
3.23546205570788));
#172202=CARTESIAN_POINT('Ctrl Pts',(20.6969527322443,-18.1591411608038,
3.23819514244229));
#172203=CARTESIAN_POINT('Ctrl Pts',(20.7010217481454,-18.1692906008916,
3.2388425031233));
#172204=CARTESIAN_POINT('Ctrl Pts',(20.7075392488657,-18.1859191946397,
3.2399042286608));
#172205=CARTESIAN_POINT('Ctrl Pts',(20.7100349199889,-18.1923797261873,
3.2403170000799));
#172206=CARTESIAN_POINT('Ctrl Pts',(20.7147921113036,-18.2048767407529,
3.24111602031924));
#172207=CARTESIAN_POINT('Ctrl Pts',(20.7170578533226,-18.2109115426207,
3.24150212220492));
#172208=CARTESIAN_POINT('Ctrl Pts',(20.7222085224844,-18.2248231049034,
3.24239280256983));
#172209=CARTESIAN_POINT('Ctrl Pts',(20.7250742515243,-18.2327068140211,
3.2428980155042));
#172210=CARTESIAN_POINT('Ctrl Pts',(20.7326183448691,-18.2538514141624,
3.24425436006234));
#172211=CARTESIAN_POINT('Ctrl Pts',(20.7372115032743,-18.267142062521,3.24510830184878));
#172212=CARTESIAN_POINT('Ctrl Pts',(20.7747041130236,-18.3792348470295,
3.25232325247312));
#172213=CARTESIAN_POINT('Ctrl Pts',(20.8003997794936,-18.480280239586,3.25892146285842));
#172214=CARTESIAN_POINT('Ctrl Pts',(20.8415710643165,-18.7127349991036,
3.27426306811785));
#172215=CARTESIAN_POINT('Ctrl Pts',(20.8523843199,-18.8445354215822,3.28308291295183));
#172216=CARTESIAN_POINT('Ctrl Pts',(20.8502762805914,-19.0268220942563,
3.29498917484003));
#172217=CARTESIAN_POINT('Ctrl Pts',(20.8478984436826,-19.0771306817407,
3.29824124810074));
#172218=CARTESIAN_POINT('Ctrl Pts',(20.8415135785747,-19.1539680466944,
3.30311260736189));
#172219=CARTESIAN_POINT('Ctrl Pts',(20.8387931751151,-19.1805835088037,
3.3047822372525));
#172220=CARTESIAN_POINT('Ctrl Pts',(20.8347491290615,-19.2138937958856,
3.30684364110698));
#172221=CARTESIAN_POINT('Ctrl Pts',(20.833896832304,-19.2206420669969,3.30725979942214));
#172222=CARTESIAN_POINT('Ctrl Pts',(20.8324900180221,-19.2313648987244,
3.30791861861039));
#172223=CARTESIAN_POINT('Ctrl Pts',(20.8319567066514,-19.2353421253766,
3.30816244680647));
#172224=CARTESIAN_POINT('Ctrl Pts',(20.8309247712772,-19.2428752240934,
3.30862322491539));
#172225=CARTESIAN_POINT('Ctrl Pts',(20.830428415835,-19.2464312989907,3.30884029347265));
#172226=CARTESIAN_POINT('Ctrl Pts',(20.8292664407998,-19.2546041957732,
3.30933817713624));
#172227=CARTESIAN_POINT('Ctrl Pts',(20.8285946086494,-19.2592200898561,
3.30961863816703));
#172228=CARTESIAN_POINT('Ctrl Pts',(20.8267562266423,-19.271564493191,3.31036680757182));
#172229=CARTESIAN_POINT('Ctrl Pts',(20.8255621107907,-19.2792889097217,
3.310833000746));
#172230=CARTESIAN_POINT('Ctrl Pts',(20.8164287987521,-19.3362776034545,
3.31425907681197));
#172231=CARTESIAN_POINT('Ctrl Pts',(20.8067921061513,-19.3852582527571,
3.31712994017732));
#172232=CARTESIAN_POINT('Ctrl Pts',(20.7897351449627,-19.4582297187077,
3.32135674762059));
#172233=CARTESIAN_POINT('Ctrl Pts',(20.7836059566652,-19.4825007122062,
3.32275412859375));
#172234=CARTESIAN_POINT('Ctrl Pts',(20.7393513635755,-19.6455097222503,
3.33211511171528));
#172235=CARTESIAN_POINT('Ctrl Pts',(20.6875982112282,-19.7801585200771,
3.33975532083144));
#172236=CARTESIAN_POINT('Ctrl Pts',(20.5946491093862,-19.9636802394936,
3.3511356401834));
#172237=CARTESIAN_POINT('Ctrl Pts',(20.564311068918,-20.0175855415329,3.35460516621097));
#172238=CARTESIAN_POINT('Ctrl Pts',(20.5119764095494,-20.1017294375973,
3.36029176480344));
#172239=CARTESIAN_POINT('Ctrl Pts',(20.4914623268213,-20.1328487678449,
3.36245762587111));
#172240=CARTESIAN_POINT('Ctrl Pts',(20.463766235496,-20.1725415919741,3.36531069886447));
#172241=CARTESIAN_POINT('Ctrl Pts',(20.4573221120493,-20.1816234782072,
3.3659698165557));
#172242=CARTESIAN_POINT('Ctrl Pts',(20.4467284701655,-20.1963065423077,
3.3670459714976));
#172243=CARTESIAN_POINT('Ctrl Pts',(20.4426223591354,-20.2019388848348,
3.36746133058823));
#172244=CARTESIAN_POINT('Ctrl Pts',(20.434674560547,-20.2127285173225,3.36826198986839));
#172245=CARTESIAN_POINT('Ctrl Pts',(20.4308370364429,-20.2178887888051,
3.3686471250419));
#172246=CARTESIAN_POINT('Ctrl Pts',(20.4219994872438,-20.2296601415075,
3.36953079444804));
#172247=CARTESIAN_POINT('Ctrl Pts',(20.4169840502601,-20.2362594713105,
3.37002993074997));
#172248=CARTESIAN_POINT('Ctrl Pts',(20.4035631274798,-20.2537051342916,
3.37135945867928));
#172249=CARTESIAN_POINT('Ctrl Pts',(20.3950908262364,-20.2644993509937,
3.37219248885101));
#172250=CARTESIAN_POINT('Ctrl Pts',(20.3301141934909,-20.3456465592972,
3.37853531216837));
#172251=CARTESIAN_POINT('Ctrl Pts',(20.2692759214737,-20.4123956236509,
3.38422123195241));
#172252=CARTESIAN_POINT('Ctrl Pts',(20.1040429515391,-20.5719132815576,
3.3990491691745));
#172253=CARTESIAN_POINT('Ctrl Pts',(19.9943909845992,-20.6586183970893,
3.40836597789303));
#172254=CARTESIAN_POINT('Ctrl Pts',(19.8304355719691,-20.7637896475959,
3.42112380011482));
#172255=CARTESIAN_POINT('Ctrl Pts',(19.7826887939228,-20.7918384016435,
3.42471118619517));
#172256=CARTESIAN_POINT('Ctrl Pts',(19.708770732619,-20.8314476486225,3.43001917987131));
#172257=CARTESIAN_POINT('Ctrl Pts',(19.6833761934619,-20.8444023022816,
3.43180054543422));
#172258=CARTESIAN_POINT('Ctrl Pts',(19.6514772289623,-20.8598712665299,
3.43397918279146));
#172259=CARTESIAN_POINT('Ctrl Pts',(19.6452131115392,-20.862870980407,3.43440422055783));
#172260=CARTESIAN_POINT('Ctrl Pts',(19.635277757715,-20.8675687830322,3.43507382443312));
#172261=CARTESIAN_POINT('Ctrl Pts',(19.6316162868592,-20.8692872401593,
3.4353196229997));
#172262=CARTESIAN_POINT('Ctrl Pts',(19.6247017322823,-20.8725083348189,
3.4357819455412));
#172263=CARTESIAN_POINT('Ctrl Pts',(19.6214497987299,-20.8740131880172,
3.4359986004432));
#172264=CARTESIAN_POINT('Ctrl Pts',(19.6140065032312,-20.87743470274,3.43649274590803));
#172265=CARTESIAN_POINT('Ctrl Pts',(19.6098126979085,-20.8793459366048,
3.43676990072171));
#172266=CARTESIAN_POINT('Ctrl Pts',(19.5986629934554,-20.8843832600036,
3.43750348515486));
#172267=CARTESIAN_POINT('Ctrl Pts',(19.5916963144821,-20.8874855183854,
3.43795849113888));
#172268=CARTESIAN_POINT('Ctrl Pts',(19.5428156064377,-20.9089363175357,
3.44112854378698));
#172269=CARTESIAN_POINT('Ctrl Pts',(19.5003298265819,-20.9259609175579,
3.44376885334204));
#172270=CARTESIAN_POINT('Ctrl Pts',(19.4510875086233,-20.9438630767841,
3.44673522128603));
#172271=CARTESIAN_POINT('Ctrl Pts',(19.4448419538897,-20.9461004813692,
3.44710975171836));
#172272=CARTESIAN_POINT('Ctrl Pts',(19.4352870203563,-20.9494728417585,
3.44768028399848));
#172273=CARTESIAN_POINT('Ctrl Pts',(19.4319852141408,-20.9506289999753,
3.44787699140494));
#172274=CARTESIAN_POINT('Ctrl Pts',(19.2892700983293,-21.0002052354252,
3.45636069395331));
#172275=CARTESIAN_POINT('Ctrl Pts',(19.1451709770689,-21.0339254455784,
3.46418597921613));
#172276=CARTESIAN_POINT('Ctrl Pts',(18.9017618184516,-21.0646042777067,
3.47766679983518));
#172277=CARTESIAN_POINT('Ctrl Pts',(18.8040761841515,-21.0700951211588,
3.48313953588566));
#172278=CARTESIAN_POINT('Ctrl Pts',(18.684700857321,-21.0685368217708,3.4900893661415));
#172279=CARTESIAN_POINT('Ctrl Pts',(18.6630404565635,-21.0679213632152,
3.49136056928072));
#172280=CARTESIAN_POINT('Ctrl Pts',(18.6323461967869,-21.0665773861516,
3.49317781885006));
#172281=CARTESIAN_POINT('Ctrl Pts',(18.6233012462277,-21.0661231751636,
3.49371527734835));
#172282=CARTESIAN_POINT('Ctrl Pts',(18.6077351090038,-21.0652413214848,
3.49464370028917));
#172283=CARTESIAN_POINT('Ctrl Pts',(18.6012124276154,-21.0648414906643,
3.49503378731128));
#172284=CARTESIAN_POINT('Ctrl Pts',(18.5887492848719,-21.0640195776363,
3.49578118851852));
#172285=CARTESIAN_POINT('Ctrl Pts',(18.5828085397848,-21.0636026159759,
3.49613833815913));
#172286=CARTESIAN_POINT('Ctrl Pts',(18.5674132547923,-21.0624567694386,
3.49706622564269));
#172287=CARTESIAN_POINT('Ctrl Pts',(18.5579617882873,-21.0616894233012,
3.49763816723172));
#172288=CARTESIAN_POINT('Ctrl Pts',(18.5259974681395,-21.0588780102242,
3.49958037477924));
#172289=CARTESIAN_POINT('Ctrl Pts',(18.5035129097444,-21.0565369187251,
3.50095992805857));
#172290=CARTESIAN_POINT('Ctrl Pts',(18.3020350626346,-21.0322916299343,
3.51344598259085));
#172291=CARTESIAN_POINT('Ctrl Pts',(18.1265177211764,-20.9879633804279,
3.52530095484291));
#172292=CARTESIAN_POINT('Ctrl Pts',(17.8809191597038,-20.8913151870048,
3.54273408455607));
#172293=CARTESIAN_POINT('Ctrl Pts',(17.8049369818549,-20.8560835191905,
3.54824059949552));
#172294=CARTESIAN_POINT('Ctrl Pts',(17.6986805839837,-20.7989350608254,
3.55593786516203));
#172295=CARTESIAN_POINT('Ctrl Pts',(17.6665872714109,-20.7805748176268,
3.55826173359992));
#172296=CARTESIAN_POINT('Ctrl Pts',(17.6285600993605,-20.7574772796631,
3.56099931633537));
#172297=CARTESIAN_POINT('Ctrl Pts',(17.6221518087216,-20.7535380053606,
3.56146008983523));
#172298=CARTESIAN_POINT('Ctrl Pts',(17.6122225228686,-20.7473611594343,
3.56217299124678));
#172299=CARTESIAN_POINT('Ctrl Pts',(17.6086869895072,-20.7451472416156,
3.56242662828347));
#172300=CARTESIAN_POINT('Ctrl Pts',(17.6021423731771,-20.7410220846892,
3.56289571687127));
#172301=CARTESIAN_POINT('Ctrl Pts',(17.5991316008057,-20.7391137131423,
3.56311134663739));
#172302=CARTESIAN_POINT('Ctrl Pts',(17.5923358765432,-20.7347821588739,
3.56359768294462));
#172303=CARTESIAN_POINT('Ctrl Pts',(17.5885538222792,-20.7323545297463,
3.5638680896978));
#172304=CARTESIAN_POINT('Ctrl Pts',(17.5774135297954,-20.7251535928498,
3.5646639223471));
#172305=CARTESIAN_POINT('Ctrl Pts',(17.5700770883693,-20.7203465126205,
3.56518715377071));
#172306=CARTESIAN_POINT('Ctrl Pts',(17.5172400270725,-20.6852546301564,
3.56895081440199));
#172307=CARTESIAN_POINT('Ctrl Pts',(17.4728933733905,-20.6532605943579,
3.57208475553217));
#172308=CARTESIAN_POINT('Ctrl Pts',(17.2972506856308,-20.5158954866961,
3.58461109173557));
#172309=CARTESIAN_POINT('Ctrl Pts',(17.1775027564072,-20.3967634918128,
3.59346953744706));
#172310=CARTESIAN_POINT('Ctrl Pts',(17.0365790293146,-20.2184613731332,
3.60606881771752));
#172311=CARTESIAN_POINT('Ctrl Pts',(17.0019838239229,-20.1707212819433,
3.60938273522733));
#172312=CARTESIAN_POINT('Ctrl Pts',(16.9495309616789,-20.0915859337807,
3.61483688239362));
#172313=CARTESIAN_POINT('Ctrl Pts',(16.9304052155671,-20.0610678412497,
3.61693119579561));
#172314=CARTESIAN_POINT('Ctrl Pts',(16.9064660217075,-20.0206110442278,
3.6197028083194));
#172315=CARTESIAN_POINT('Ctrl Pts',(16.9009381177284,-20.0111006253011,
3.62035400052919));
#172316=CARTESIAN_POINT('Ctrl Pts',(16.8920438741355,-19.9955203868616,
3.62142042708464));
#172317=CARTESIAN_POINT('Ctrl Pts',(16.8886327781257,-19.9894762561496,
3.62183404056539));
#172318=CARTESIAN_POINT('Ctrl Pts',(16.8821134427118,-19.9777907507361,
3.62263357975897));
#172319=CARTESIAN_POINT('Ctrl Pts',(16.8790011034011,-19.9721517424166,
3.62301935259321));
#172320=CARTESIAN_POINT('Ctrl Pts',(16.8719106576768,-19.9591653735746,
3.62390768280936));
#172321=CARTESIAN_POINT('Ctrl Pts',(16.8679502368883,-19.9518085251618,
3.62441086379798));
#172322=CARTESIAN_POINT('Ctrl Pts',(16.857494875827,-19.9321081894115,3.62575822111199));
#172323=CARTESIAN_POINT('Ctrl Pts',(16.8510782832184,-19.919723792131,3.6266051495001));
#172324=CARTESIAN_POINT('Ctrl Pts',(16.8001375194838,-19.8189801749733,
3.6334951568589));
#172325=CARTESIAN_POINT('Ctrl Pts',(16.7617417033069,-19.7276745962983,
3.6397514818284));
#172326=CARTESIAN_POINT('Ctrl Pts',(16.6860055055724,-19.5051258936198,
3.65499319442853));
#172327=CARTESIAN_POINT('Ctrl Pts',(16.6546777501633,-19.3722916901845,
3.66409684717405));
#172328=CARTESIAN_POINT('Ctrl Pts',(16.6262468690777,-19.1633139088278,
3.67787830905605));
#172329=CARTESIAN_POINT('Ctrl Pts',(16.6200989473124,-19.0887539837339,
3.6826851014469));
#172330=CARTESIAN_POINT('Ctrl Pts',(16.617649085885,-19.0051628103158,3.68784414639839));
#172331=CARTESIAN_POINT('Ctrl Pts',(16.6174451480529,-18.99630621939,3.68838785288456));
#172332=CARTESIAN_POINT('Ctrl Pts',(16.6172222390634,-18.9829958379578,
3.68920035586386));
#172333=CARTESIAN_POINT('Ctrl Pts',(16.6171617202317,-18.978542971068,3.6894713942079));
#172334=CARTESIAN_POINT('Ctrl Pts',(16.6170816555799,-18.9708703404116,
3.68993703635941));
#172335=CARTESIAN_POINT('Ctrl Pts',(16.6170554039629,-18.9676507020389,
3.69013201251977));
#172336=CARTESIAN_POINT('Ctrl Pts',(16.6170125976391,-18.960360878647,3.6905725165307));
#172337=CARTESIAN_POINT('Ctrl Pts',(16.6170004354008,-18.956290708061,3.69081779563898));
#172338=CARTESIAN_POINT('Ctrl Pts',(16.6169992761381,-18.9451601459764,
3.69148678110644));
#172339=CARTESIAN_POINT('Ctrl Pts',(16.6170338608871,-18.9380997307795,
3.69190918767181));
#172340=CARTESIAN_POINT('Ctrl Pts',(16.6174008065129,-18.901040209158,3.69411674773463));
#172341=CARTESIAN_POINT('Ctrl Pts',(16.6183355257536,-18.8710488603327,
3.69587020225227));
#172342=CARTESIAN_POINT('Ctrl Pts',(16.6230423750926,-18.7813334126221,
3.70104314768622));
#172343=CARTESIAN_POINT('Ctrl Pts',(16.6287093235971,-18.721736293826,3.70438373877959));
#172344=CARTESIAN_POINT('Ctrl Pts',(16.6574679273623,-18.5134441951214,
3.7159609037468));
#172345=CARTESIAN_POINT('Ctrl Pts',(16.6938573090406,-18.3671015374049,
3.72394888845156));
#172346=CARTESIAN_POINT('Ctrl Pts',(16.7454193692324,-18.2258897639231,
3.73234496387082));
#172347=CARTESIAN_POINT('Origin',(18.734,-18.952,0.));
#172348=CARTESIAN_POINT('',(16.7454193672347,-18.225889769394,4.75730093103984));
#172349=CARTESIAN_POINT('',(16.7454193964829,-18.2258896892926,4.53222340662745));
#172350=CARTESIAN_POINT('',(16.7454193692319,-18.2258897639242,0.));
#172351=CARTESIAN_POINT('',(16.6170000778093,-18.952573972551,4.70909170728562));
#172352=CARTESIAN_POINT('Ctrl Pts',(16.7454193672347,-18.225889769394,4.75730093103984));
#172353=CARTESIAN_POINT('Ctrl Pts',(16.7303995485604,-18.2670241857187,
4.75455315814197));
#172354=CARTESIAN_POINT('Ctrl Pts',(16.7166594239208,-18.3086153643389,
4.75176655660383));
#172355=CARTESIAN_POINT('Ctrl Pts',(16.646312753438,-18.5460434110503,4.73582624675881));
#172356=CARTESIAN_POINT('Ctrl Pts',(16.6169448256217,-18.7487856962723,
4.72195810323501));
#172357=CARTESIAN_POINT('Ctrl Pts',(16.6170000778093,-18.952573972551,4.70909170728562));
#172358=CARTESIAN_POINT('Ctrl Pts',(16.6170000784466,-18.9525763185082,
4.70909155917109));
#172359=CARTESIAN_POINT('Ctrl Pts',(16.6170043638029,-18.9683177858256,
4.70809770510508));
#172360=CARTESIAN_POINT('Ctrl Pts',(16.6171842235391,-18.9840592810225,
4.70711097584169));
#172361=CARTESIAN_POINT('Ctrl Pts',(16.6177851446519,-19.0106677086203,
4.70545672920642));
#172362=CARTESIAN_POINT('Ctrl Pts',(16.6181143694088,-19.0215357710275,
4.70478491638385));
#172363=CARTESIAN_POINT('Ctrl Pts',(16.6187085002744,-19.0371682452493,
4.70382459956396));
#172364=CARTESIAN_POINT('Ctrl Pts',(16.6189057981575,-19.0419348494304,
4.70353258719135));
#172365=CARTESIAN_POINT('Ctrl Pts',(16.6192791186492,-19.0502719316248,
4.70302329503004));
#172366=CARTESIAN_POINT('Ctrl Pts',(16.6194480742848,-19.0538426848307,
4.70280563353445));
#172367=CARTESIAN_POINT('Ctrl Pts',(16.6197955283407,-19.0608119166624,
4.70238174654777));
#172368=CARTESIAN_POINT('Ctrl Pts',(16.6199731789209,-19.0642104344126,
4.70217547433106));
#172369=CARTESIAN_POINT('Ctrl Pts',(16.6203449448697,-19.0710079765581,
4.70176378523197));
#172370=CARTESIAN_POINT('Ctrl Pts',(16.6205390643402,-19.0744069621433,
4.70155836834217));
#172371=CARTESIAN_POINT('Ctrl Pts',(16.6210263189166,-19.0825917791343,
4.7010647506778));
#172372=CARTESIAN_POINT('Ctrl Pts',(16.6213275167566,-19.087377137277,4.70077699901608));
#172373=CARTESIAN_POINT('Ctrl Pts',(16.6224923816379,-19.1049326605121,
4.69972433448047));
#172374=CARTESIAN_POINT('Ctrl Pts',(16.6234556165371,-19.1176962417628,
4.69896478990194));
#172375=CARTESIAN_POINT('Ctrl Pts',(16.626705176885,-19.1561092997692,4.69669421515918));
#172376=CARTESIAN_POINT('Ctrl Pts',(16.6293438484297,-19.1817274135841,
4.69520056233799));
#172377=CARTESIAN_POINT('Ctrl Pts',(16.6557757821633,-19.3993135917065,
4.68264215644977));
#172378=CARTESIAN_POINT('Ctrl Pts',(16.705310468741,-19.5872492273014,4.67256750562623));
#172379=CARTESIAN_POINT('Ctrl Pts',(16.8017752320132,-19.8188889000282,
4.65864103069371));
#172380=CARTESIAN_POINT('Ctrl Pts',(16.8260072394902,-19.8709950098483,
4.65540741632111));
#172381=CARTESIAN_POINT('Ctrl Pts',(16.868526570959,-19.9534728106902,4.65007368184504));
#172382=CARTESIAN_POINT('Ctrl Pts',(16.8855103020577,-19.9844846377123,
4.64801687137834));
#172383=CARTESIAN_POINT('Ctrl Pts',(16.9087490825874,-20.024505243469,4.64528803022755));
#172384=CARTESIAN_POINT('Ctrl Pts',(16.9143093172387,-20.0339122982393,
4.64464109505808));
#172385=CARTESIAN_POINT('Ctrl Pts',(16.9235113715937,-20.0492091283716,
4.64357989145143));
#172386=CARTESIAN_POINT('Ctrl Pts',(16.9271097445465,-20.0551249013447,
4.64316721341621));
#172387=CARTESIAN_POINT('Ctrl Pts',(16.9341142634616,-20.0665141972177,
4.64236824973311));
#172388=CARTESIAN_POINT('Ctrl Pts',(16.937516520852,-20.0719900303649,4.64198211035626));
#172389=CARTESIAN_POINT('Ctrl Pts',(16.945405197213,-20.0845581927722,4.64109116471016));
#172390=CARTESIAN_POINT('Ctrl Pts',(16.9499088621105,-20.0916395206857,
4.64058572276215));
#172391=CARTESIAN_POINT('Ctrl Pts',(16.9620781834053,-20.1105249993702,
4.63922836415674));
#172392=CARTESIAN_POINT('Ctrl Pts',(16.9698195535821,-20.122279639979,4.6383736307449));
#172393=CARTESIAN_POINT('Ctrl Pts',(17.06429528615,-20.2626654609611,4.62804424042255));
#172394=CARTESIAN_POINT('Ctrl Pts',(17.1647816944768,-20.3814384148935,
4.61801768707867));
#172395=CARTESIAN_POINT('Ctrl Pts',(17.3590117104694,-20.5656208243941,
4.60036158904024));
#172396=CARTESIAN_POINT('Ctrl Pts',(17.4467608782599,-20.636453150459,4.59287092259428));
#172397=CARTESIAN_POINT('Ctrl Pts',(17.5637595002678,-20.7163903003474,
4.58378140617193));
#172398=CARTESIAN_POINT('Ctrl Pts',(17.5881262370498,-20.7323116152937,
4.58193408903708));
#172399=CARTESIAN_POINT('Ctrl Pts',(17.6231389365486,-20.7541722558661,
4.57935189551883));
#172400=CARTESIAN_POINT('Ctrl Pts',(17.6335188495791,-20.7605293458116,
4.57859517006848));
#172401=CARTESIAN_POINT('Ctrl Pts',(17.6495558788656,-20.7701618909621,
4.57744015720231));
#172402=CARTESIAN_POINT('Ctrl Pts',(17.6551741228333,-20.7735011509362,
4.57703815948451));
#172403=CARTESIAN_POINT('Ctrl Pts',(17.6644973636086,-20.778984245074,4.57637552990331));
#172404=CARTESIAN_POINT('Ctrl Pts',(17.6681935141098,-20.781142929451,4.57611398885691));
#172405=CARTESIAN_POINT('Ctrl Pts',(17.6753592979093,-20.7852989092982,
4.57560920505075));
#172406=CARTESIAN_POINT('Ctrl Pts',(17.6788280964909,-20.787297600286,4.57536587445251));
#172407=CARTESIAN_POINT('Ctrl Pts',(17.6853320064863,-20.791020561042,4.57491158035356));
#172408=CARTESIAN_POINT('Ctrl Pts',(17.6883656789565,-20.7927471448914,
4.57470047235492));
#172409=CARTESIAN_POINT('Ctrl Pts',(17.6953670040798,-20.7967089845245,
4.57421506945905));
#172410=CARTESIAN_POINT('Ctrl Pts',(17.6993376008,-20.7989389427837,4.57394111666568));
#172411=CARTESIAN_POINT('Ctrl Pts',(17.711491303497,-20.8057131865469,4.57310652566121));
#172412=CARTESIAN_POINT('Ctrl Pts',(17.7196975057545,-20.8102160988045,
4.57254847128136));
#172413=CARTESIAN_POINT('Ctrl Pts',(17.7893103843811,-20.8478155623358,
4.5678582229013));
#172414=CARTESIAN_POINT('Ctrl Pts',(17.8522951891491,-20.8779163613929,
4.56390018414421));
#172415=CARTESIAN_POINT('Ctrl Pts',(18.0595667820946,-20.9646672314175,
4.55141655729296));
#172416=CARTESIAN_POINT('Ctrl Pts',(18.2086110102818,-21.0086136308057,
4.54321803304844));
#172417=CARTESIAN_POINT('Ctrl Pts',(18.4384407830901,-21.0497376837955,
4.53025828619843));
#172418=CARTESIAN_POINT('Ctrl Pts',(18.516462534563,-21.0592575011268,4.52581277617519));
#172419=CARTESIAN_POINT('Ctrl Pts',(18.6140626697009,-21.0656876860543,
4.5201045287648));
#172420=CARTESIAN_POINT('Ctrl Pts',(18.6333137505489,-21.066692138403,4.51897170862239));
#172421=CARTESIAN_POINT('Ctrl Pts',(18.6612089919008,-21.067765846773,4.51731923100289));
#172422=CARTESIAN_POINT('Ctrl Pts',(18.6698444313525,-21.0680452993421,
4.51680615627028));
#172423=CARTESIAN_POINT('Ctrl Pts',(18.684941803863,-21.0684413672396,4.51590639225528));
#172424=CARTESIAN_POINT('Ctrl Pts',(18.6914030507339,-21.068581268474,4.51552043768356));
#172425=CARTESIAN_POINT('Ctrl Pts',(18.703917197826,-21.0687949044309,4.5147711758953));
#172426=CARTESIAN_POINT('Ctrl Pts',(18.7099699792689,-21.0688722680718,
4.51440798631822));
#172427=CARTESIAN_POINT('Ctrl Pts',(18.7243874261361,-21.0689947018708,
4.51354096797064));
#172428=CARTESIAN_POINT('Ctrl Pts',(18.7327521432728,-21.0690161570091,
4.51303640365485));
#172429=CARTESIAN_POINT('Ctrl Pts',(18.7626368289217,-21.0689156937115,
4.51122812784682));
#172430=CARTESIAN_POINT('Ctrl Pts',(18.7841539744868,-21.0685152131365,
4.50991573833505));
#172431=CARTESIAN_POINT('Ctrl Pts',(18.9965843735425,-21.061320298692,4.49685197832337));
#172432=CARTESIAN_POINT('Ctrl Pts',(19.1857206933902,-21.0290414067206,
4.48424637383756));
#172433=CARTESIAN_POINT('Ctrl Pts',(19.4410388815917,-20.9489123845725,
4.46658973483107));
#172434=CARTESIAN_POINT('Ctrl Pts',(19.512869515398,-20.9220068351225,4.46156254636189));
#172435=CARTESIAN_POINT('Ctrl Pts',(19.6152121508221,-20.8771971407868,
4.45444673571601));
#172436=CARTESIAN_POINT('Ctrl Pts',(19.6469852845929,-20.8623342869692,
4.45224483594233));
#172437=CARTESIAN_POINT('Ctrl Pts',(19.6850057934403,-20.8433835800545,
4.44963159486516));
#172438=CARTESIAN_POINT('Ctrl Pts',(19.6916178345808,-20.8400444784696,
4.44917794123936));
#172439=CARTESIAN_POINT('Ctrl Pts',(19.7019036798692,-20.8347821592329,
4.44847365066999));
#172440=CARTESIAN_POINT('Ctrl Pts',(19.7055895148865,-20.8328827735597,
4.44822156158979));
#172441=CARTESIAN_POINT('Ctrl Pts',(19.7124359161086,-20.8293291887992,
4.44775387671116));
#172442=CARTESIAN_POINT('Ctrl Pts',(19.7155978504593,-20.8276778468827,
4.44753811186874));
#172443=CARTESIAN_POINT('Ctrl Pts',(19.722764064781,-20.8239121582036,4.44704961076768));
#172444=CARTESIAN_POINT('Ctrl Pts',(19.7267657345108,-20.8217929567438,
4.44677718577642));
#172445=CARTESIAN_POINT('Ctrl Pts',(19.7371070772479,-20.8162738375559,
4.4460740175249));
#172446=CARTESIAN_POINT('Ctrl Pts',(19.7434363348632,-20.8128543841525,
4.44564448243856));
#172447=CARTESIAN_POINT('Ctrl Pts',(19.7827708128028,-20.7913437428229,
4.44297945114501));
#172448=CARTESIAN_POINT('Ctrl Pts',(19.8153083216276,-20.7724060884381,
4.44079430449092));
#172449=CARTESIAN_POINT('Ctrl Pts',(19.9918623416976,-20.6632418768566,
4.42894868656502));
#172450=CARTESIAN_POINT('Ctrl Pts',(20.1251254953532,-20.5567890886888,
4.42000617243612));
#172451=CARTESIAN_POINT('Ctrl Pts',(20.3107781992903,-20.3677953346874,
4.40543016990868));
#172452=CARTESIAN_POINT('Ctrl Pts',(20.3726815773034,-20.2956612544309,
4.40010468937925));
#172453=CARTESIAN_POINT('Ctrl Pts',(20.4423084910402,-20.2025304762003,
4.39333330054994));
#172454=CARTESIAN_POINT('Ctrl Pts',(20.4548266656395,-20.1852477084033,
4.39208111542018));
#172455=CARTESIAN_POINT('Ctrl Pts',(20.4722503311395,-20.1604104452995,
4.39028641694498));
#172456=CARTESIAN_POINT('Ctrl Pts',(20.4773724369796,-20.1530089758969,
4.38975220026931));
#172457=CARTESIAN_POINT('Ctrl Pts',(20.486125853098,-20.1401862514727,4.38882762053508));
#172458=CARTESIAN_POINT('Ctrl Pts',(20.4897796137966,-20.1347804190083,
4.38843811564798));
#172459=CARTESIAN_POINT('Ctrl Pts',(20.4967266216542,-20.1243990184244,
4.38769060519103));
#172460=CARTESIAN_POINT('Ctrl Pts',(20.5000239434974,-20.1194262421892,
4.38733275824559));
#172461=CARTESIAN_POINT('Ctrl Pts',(20.5085413668962,-20.1064622324682,
4.38640037710397));
#172462=CARTESIAN_POINT('Ctrl Pts',(20.5137284798246,-20.0984495812965,
4.38582461579452));
#172463=CARTESIAN_POINT('Ctrl Pts',(20.5312210626313,-20.0710235705581,
4.38385544930948));
#172464=CARTESIAN_POINT('Ctrl Pts',(20.5432641432144,-20.0514455394227,
4.3824524023307));
#172465=CARTESIAN_POINT('Ctrl Pts',(20.6445550676644,-19.8806078581306,
4.37022777195926));
#172466=CARTESIAN_POINT('Ctrl Pts',(20.7149615076516,-19.7190079758745,
4.35870127227442));
#172467=CARTESIAN_POINT('Ctrl Pts',(20.789180103058,-19.4672456659107,4.34135943388337));
#172468=CARTESIAN_POINT('Ctrl Pts',(20.8086009619582,-19.3824371213776,
4.33563141146094));
#172469=CARTESIAN_POINT('Ctrl Pts',(20.8289075833434,-19.2593759109716,
4.32766841159355));
#172470=CARTESIAN_POINT('Ctrl Pts',(20.8340621234775,-19.2219207666357,
4.32529081759885));
#172471=CARTESIAN_POINT('Ctrl Pts',(20.839042052748,-19.1768205202957,4.3224986811117));
#172472=CARTESIAN_POINT('Ctrl Pts',(20.8398325609285,-19.1692913700373,
4.32203491438735));
#172473=CARTESIAN_POINT('Ctrl Pts',(20.8409970358603,-19.1575966428738,
4.32131839546422));
#172474=CARTESIAN_POINT('Ctrl Pts',(20.8413990669954,-19.1534340135387,
4.32106410990473));
#172475=CARTESIAN_POINT('Ctrl Pts',(20.8421208487724,-19.1457219329353,
4.32059442465788));
#172476=CARTESIAN_POINT('Ctrl Pts',(20.8424439689266,-19.1421728963991,
4.32037884293414));
#172477=CARTESIAN_POINT('Ctrl Pts',(20.8431530945784,-19.1341600862371,
4.31989337473308));
#172478=CARTESIAN_POINT('Ctrl Pts',(20.8435338914737,-19.1296959058606,
4.3196237833973));
#172479=CARTESIAN_POINT('Ctrl Pts',(20.8444763573567,-19.1182169271714,
4.31893274822383));
#172480=CARTESIAN_POINT('Ctrl Pts',(20.8450172319542,-19.1112004125795,
4.31851244417552));
#172481=CARTESIAN_POINT('Ctrl Pts',(20.848048910714,-19.0691356968986,4.31600450809082));
#172482=CARTESIAN_POINT('Ctrl Pts',(20.8497019886367,-19.0340304003715,
4.31396066853021));
#172483=CARTESIAN_POINT('Ctrl Pts',(20.8508317907905,-18.9830430664197,
4.31104263089572));
#172484=CARTESIAN_POINT('Ctrl Pts',(20.8510049507799,-18.9671843196658,
4.3101421031561));
#172485=CARTESIAN_POINT('Ctrl Pts',(20.8509917276277,-18.9257264327126,
4.30780306630794));
#172486=CARTESIAN_POINT('Ctrl Pts',(20.8505192678903,-18.9001296074882,
4.30637396114873));
#172487=CARTESIAN_POINT('Ctrl Pts',(20.847950390662,-18.8299622870072,4.30248318612837));
#172488=CARTESIAN_POINT('Ctrl Pts',(20.8449090787682,-18.7854390923712,
4.3000438789528));
#172489=CARTESIAN_POINT('Ctrl Pts',(20.829567578654,-18.6322491769349,4.29166191353768));
#172490=CARTESIAN_POINT('Ctrl Pts',(20.8102598944457,-18.5244628304246,
4.28577433985349));
#172491=CARTESIAN_POINT('Ctrl Pts',(20.7636477950918,-18.3454140539896,
4.2754866413596));
#172492=CARTESIAN_POINT('Ctrl Pts',(20.7406691328952,-18.2732556217367,
4.27119645027553));
#172493=CARTESIAN_POINT('Ctrl Pts',(20.7071891610852,-18.1848164968621,
4.26567544465709));
#172494=CARTESIAN_POINT('Ctrl Pts',(20.7002636503135,-18.1672368407426,
4.26456479443249));
#172495=CARTESIAN_POINT('Ctrl Pts',(20.689856181517,-18.1418215957923,4.26293886638913));
#172496=CARTESIAN_POINT('Ctrl Pts',(20.6865603448444,-18.1339104291894,
4.26242987456728));
#172497=CARTESIAN_POINT('Ctrl Pts',(20.6806993452425,-18.1200791597766,
4.26153484398041));
#172498=CARTESIAN_POINT('Ctrl Pts',(20.6781549711503,-18.1141503285822,
4.26114951645581));
#172499=CARTESIAN_POINT('Ctrl Pts',(20.6731630380808,-18.1026634391019,
4.26039967421896));
#172500=CARTESIAN_POINT('Ctrl Pts',(20.6707185834004,-18.0971040943756,
4.26003526867241));
#172501=CARTESIAN_POINT('Ctrl Pts',(20.6648198327366,-18.0838439032243,
4.25916245376206));
#172502=CARTESIAN_POINT('Ctrl Pts',(20.6613433584442,-18.0761530896946,
4.25865328614023));
#172503=CARTESIAN_POINT('Ctrl Pts',(20.6486448480703,-18.0485026074533,
4.25681193685448));
#172504=CARTESIAN_POINT('Ctrl Pts',(20.6391582333856,-18.0286666468042,
4.25547065783859));
#172505=CARTESIAN_POINT('Ctrl Pts',(20.546145041176,-17.8417200226915,4.24263097866432));
#172506=CARTESIAN_POINT('Ctrl Pts',(20.4411650382425,-17.6862390983626,
4.23032107809196));
#172507=CARTESIAN_POINT('Ctrl Pts',(20.2645139983812,-17.4872434911663,
4.21275533868005));
#172508=CARTESIAN_POINT('Ctrl Pts',(20.2085405373111,-17.4309093964385,
4.20754406201707));
#172509=CARTESIAN_POINT('Ctrl Pts',(20.1229033879014,-17.3539014600333,
4.20020386615802));
#172510=CARTESIAN_POINT('Ctrl Pts',(20.0956684954129,-17.3306330380802,
4.19795417072745));
#172511=CARTESIAN_POINT('Ctrl Pts',(20.0620669148646,-17.3033694112692,
4.19529212064689));
#172512=CARTESIAN_POINT('Ctrl Pts',(20.0562544412648,-17.2987039754446,
4.19483562144942));
#172513=CARTESIAN_POINT('Ctrl Pts',(20.0471622419283,-17.2914846576279,
4.19412788839423));
#172514=CARTESIAN_POINT('Ctrl Pts',(20.0438994953154,-17.2889096270083,
4.19387517973555));
#172515=CARTESIAN_POINT('Ctrl Pts',(20.0378233134293,-17.2841431462135,
4.19340693652406));
#172516=CARTESIAN_POINT('Ctrl Pts',(20.035011951709,-17.281949216596,4.19319122924798));
#172517=CARTESIAN_POINT('Ctrl Pts',(20.028629118394,-17.2769940822256,4.1927036105747));
#172518=CARTESIAN_POINT('Ctrl Pts',(20.025054359683,-17.2742371979377,4.19243200578278));
#172519=CARTESIAN_POINT('Ctrl Pts',(20.0144335225311,-17.2661003635453,
4.19162936538449));
#172520=CARTESIAN_POINT('Ctrl Pts',(20.0073623383546,-17.2607531370939,
4.19110058062748));
#172521=CARTESIAN_POINT('Ctrl Pts',(19.9544663864566,-17.2212730640029,
4.18718478482324));
#172522=CARTESIAN_POINT('Ctrl Pts',(19.9073057639961,-17.1889603693999,
4.18391425916349));
#172523=CARTESIAN_POINT('Ctrl Pts',(19.7306463782179,-17.0781530767405,
4.17222267625575));
#172524=CARTESIAN_POINT('Ctrl Pts',(19.5941380576055,-17.0116973506049,
4.16420735934564));
#172525=CARTESIAN_POINT('Ctrl Pts',(19.3644839877892,-16.9289395463648,
4.15076200706893));
#172526=CARTESIAN_POINT('Ctrl Pts',(19.2753058170039,-16.9032763010901,
4.14555622103287));
#172527=CARTESIAN_POINT('Ctrl Pts',(19.164153621561,-16.879055052733,4.13892974352589));
#172528=CARTESIAN_POINT('Ctrl Pts',(19.1435027078165,-16.8748768987773,
4.13769320972292));
#172529=CARTESIAN_POINT('Ctrl Pts',(19.1139907181514,-16.869363150666,4.13591709199079));
#172530=CARTESIAN_POINT('Ctrl Pts',(19.1051777878207,-16.8677744272367,
4.13538556879195));
#172531=CARTESIAN_POINT('Ctrl Pts',(19.0899347952602,-16.8651262887952,
4.13446417536122));
#172532=CARTESIAN_POINT('Ctrl Pts',(19.0835093862001,-16.8640405529589,
4.134075147376));
#172533=CARTESIAN_POINT('Ctrl Pts',(19.0711817164841,-16.8620159791263,
4.13332751709865));
#172534=CARTESIAN_POINT('Ctrl Pts',(19.065280284217,-16.8610724332035,4.13296906844586));
#172535=CARTESIAN_POINT('Ctrl Pts',(19.0498903628258,-16.8586786168554,
4.13203283314908));
#172536=CARTESIAN_POINT('Ctrl Pts',(19.0403959443273,-16.8572678798925,
4.13145379925986));
#172537=CARTESIAN_POINT('Ctrl Pts',(19.0078133147692,-16.8526528162177,
4.12946155524423));
#172538=CARTESIAN_POINT('Ctrl Pts',(18.9846825953532,-16.8497653561907,
4.12803839513612));
#172539=CARTESIAN_POINT('Ctrl Pts',(18.7917166869458,-16.8289069079813,
4.11608809178876));
#172540=CARTESIAN_POINT('Ctrl Pts',(18.6203570807412,-16.8311701841246,
4.10489910512723));
#172541=CARTESIAN_POINT('Ctrl Pts',(18.3616263041957,-16.866049274014,4.08764702233133));
#172542=CARTESIAN_POINT('Ctrl Pts',(18.2729426564417,-16.8838412239402,
4.08168385502502));
#172543=CARTESIAN_POINT('Ctrl Pts',(18.14832615013,-16.9172593734167,4.07344069870718));
#172544=CARTESIAN_POINT('Ctrl Pts',(18.1112679246029,-16.9282933824863,
4.07100780009328));
#172545=CARTESIAN_POINT('Ctrl Pts',(18.0672905502075,-16.9427101867487,
4.06815963979157));
#172546=CARTESIAN_POINT('Ctrl Pts',(18.0600637077912,-16.9451225941346,
4.06769287816026));
#172547=CARTESIAN_POINT('Ctrl Pts',(18.0488804313078,-16.9489229288312,
4.06697274127613));
#172548=CARTESIAN_POINT('Ctrl Pts',(18.0449149172585,-16.9502836549867,
4.0667178082477));
#172549=CARTESIAN_POINT('Ctrl Pts',(18.0375868535028,-16.9528225632225,
4.06624752257099));
#172550=CARTESIAN_POINT('Ctrl Pts',(18.0342232636899,-16.9539974439549,
4.06603198408222));
#172551=CARTESIAN_POINT('Ctrl Pts',(18.0266492713103,-16.9566644643807,
4.06554736103049));
#172552=CARTESIAN_POINT('Ctrl Pts',(18.022440628305,-16.9581614372078,4.06527856706043));
#172553=CARTESIAN_POINT('Ctrl Pts',(18.0101012168159,-16.9625944906925,
4.06449185677364));
#172554=CARTESIAN_POINT('Ctrl Pts',(18.0019835443578,-16.9655671057874,
4.06397606049243));
#172555=CARTESIAN_POINT('Ctrl Pts',(17.9455379723991,-16.9866299471171,
4.06040026212017));
#172556=CARTESIAN_POINT('Ctrl Pts',(17.8978632353713,-17.0064337440309,
4.05743505602116));
#172557=CARTESIAN_POINT('Ctrl Pts',(17.8310742020106,-17.0370868022155,
4.05329619037604));
#172558=CARTESIAN_POINT('Ctrl Pts',(17.8113344771107,-17.0465195014372,
4.05207490024794));
#172559=CARTESIAN_POINT('Ctrl Pts',(17.6684450276636,-17.1175409486336,
4.04322468535368));
#172560=CARTESIAN_POINT('Ctrl Pts',(17.5514166600587,-17.1907087962064,
4.03590132363251));
#172561=CARTESIAN_POINT('Ctrl Pts',(17.3704325636644,-17.3300859112174,
4.02330710303858));
#172562=CARTESIAN_POINT('Ctrl Pts',(17.3021868055151,-17.390004575054,4.01820660161727));
#172563=CARTESIAN_POINT('Ctrl Pts',(17.2232621157577,-17.4688297945207,
4.01170749855595));
#172564=CARTESIAN_POINT('Ctrl Pts',(17.2087435020694,-17.4837645341443,
4.01048487776013));
#172565=CARTESIAN_POINT('Ctrl Pts',(17.1883296413621,-17.5053930741443,
4.008725293793));
#172566=CARTESIAN_POINT('Ctrl Pts',(17.1822523792232,-17.5119139702028,
4.00819618446423));
#172567=CARTESIAN_POINT('Ctrl Pts',(17.1718088678202,-17.5232627128226,
4.00727764100022));
#172568=CARTESIAN_POINT('Ctrl Pts',(17.1674233376777,-17.5280727094266,
4.00688903489124));
#172569=CARTESIAN_POINT('Ctrl Pts',(17.1590478582533,-17.5373443611202,
4.00614127375467));
#172570=CARTESIAN_POINT('Ctrl Pts',(17.1550545057865,-17.5418028681897,
4.00578226784526));
#172571=CARTESIAN_POINT('Ctrl Pts',(17.1446737338493,-17.5534921869244,
4.00484248117269));
#172572=CARTESIAN_POINT('Ctrl Pts',(17.1383167963132,-17.5607497737066,
4.00426043453881));
#172573=CARTESIAN_POINT('Ctrl Pts',(17.1165780864919,-17.5859134085734,
4.00224711048491));
#172574=CARTESIAN_POINT('Ctrl Pts',(17.1014467666773,-17.604032607531,4.00080559830235));
#172575=CARTESIAN_POINT('Ctrl Pts',(16.9829321781835,-17.7508725516009,
3.98918379304907));
#172576=CARTESIAN_POINT('Ctrl Pts',(16.8946451434888,-17.8910100374429,
3.97838997399393));
#172577=CARTESIAN_POINT('Ctrl Pts',(16.7945495092901,-18.1006775466402,
3.9630363229136));
#172578=CARTESIAN_POINT('Ctrl Pts',(16.7684811701782,-18.1627309458507,
3.9585902818317));
#172579=CARTESIAN_POINT('Ctrl Pts',(16.7454192997072,-18.22588995433,3.95421655704364));
#172580=CARTESIAN_POINT('',(16.6170007560322,-18.9537891450234,4.48828854762057));
#172581=CARTESIAN_POINT('Ctrl Pts',(16.7454193692323,-18.2258897639231,
3.73234496387082));
#172582=CARTESIAN_POINT('Ctrl Pts',(16.7511301832802,-18.2102496949126,
3.73327488065988));
#172583=CARTESIAN_POINT('Ctrl Pts',(16.7570271353207,-18.1946725451317,
3.73420935406355));
#172584=CARTESIAN_POINT('Ctrl Pts',(16.7847361158326,-18.1240091654445,
3.73849006986507));
#172585=CARTESIAN_POINT('Ctrl Pts',(16.8086666864644,-18.0697929867798,
3.74189144374715));
#172586=CARTESIAN_POINT('Ctrl Pts',(16.8402460970562,-18.0056728844381,
3.74609042332773));
#172587=CARTESIAN_POINT('Ctrl Pts',(16.845749776351,-17.9947383126766,3.74681280679622));
#172588=CARTESIAN_POINT('Ctrl Pts',(16.8549744676129,-17.9768000542255,
3.7480086185687));
#172589=CARTESIAN_POINT('Ctrl Pts',(16.8586405983915,-17.9697683583884,
3.74848011584894));
#172590=CARTESIAN_POINT('Ctrl Pts',(16.8653238732181,-17.9571235546143,
3.74933302844374));
#172591=CARTESIAN_POINT('Ctrl Pts',(16.868327031592,-17.9515031324552,3.74971394448125));
#172592=CARTESIAN_POINT('Ctrl Pts',(16.8748001940854,-17.9395190777573,
3.75053006324578));
#172593=CARTESIAN_POINT('Ctrl Pts',(16.8782775882242,-17.9331595489891,
3.75096552618938));
#172594=CARTESIAN_POINT('Ctrl Pts',(16.8877881918118,-17.9159765906649,
3.7521486376987));
#172595=CARTESIAN_POINT('Ctrl Pts',(16.8938838125168,-17.9051881966121,
3.75289851812423));
#172596=CARTESIAN_POINT('Ctrl Pts',(16.9256758914823,-17.8500564706596,
3.75676757293195));
#172597=CARTESIAN_POINT('Ctrl Pts',(16.952879941276,-17.8066065098667,3.75994114551695));
#172598=CARTESIAN_POINT('Ctrl Pts',(17.0774339360714,-17.6228529769686,
3.77392295900185));
#172599=CARTESIAN_POINT('Ctrl Pts',(17.1899738781833,-17.4936414503088,
3.78529468825417));
#172600=CARTESIAN_POINT('Ctrl Pts',(17.3851490490077,-17.3177536136922,
3.80257302147171));
#172601=CARTESIAN_POINT('Ctrl Pts',(17.4574748256261,-17.2606550911788,
3.80854929244341));
#172602=CARTESIAN_POINT('Ctrl Pts',(17.5412586053927,-17.2029572777869,
3.81483427635308));
#172603=CARTESIAN_POINT('Ctrl Pts',(17.5492591618462,-17.1975281042186,
3.81542831630398));
#172604=CARTESIAN_POINT('Ctrl Pts',(17.5611326745739,-17.189589001078,3.81630059267153));
#172605=CARTESIAN_POINT('Ctrl Pts',(17.5649769617597,-17.1870367059999,
3.81658157771615));
#172606=CARTESIAN_POINT('Ctrl Pts',(17.5718145078082,-17.1825292703079,
3.81707876465126));
#172607=CARTESIAN_POINT('Ctrl Pts',(17.5748044015588,-17.1805691244846,
3.817295299682));
#172608=CARTESIAN_POINT('Ctrl Pts',(17.5812240080072,-17.1763837052268,
3.81775834497569));
#172609=CARTESIAN_POINT('Ctrl Pts',(17.5846551956961,-17.1741607959522,
3.81800469784223));
#172610=CARTESIAN_POINT('Ctrl Pts',(17.594098473366,-17.168081693519,3.81867964902525));
#172611=CARTESIAN_POINT('Ctrl Pts',(17.6001237367296,-17.1642459236454,
3.81910690840493));
#172612=CARTESIAN_POINT('Ctrl Pts',(17.6325052722027,-17.1438609337127,
3.82138566269506));
#172613=CARTESIAN_POINT('Ctrl Pts',(17.6592061315552,-17.1278629739202,
3.82320297959581));
#172614=CARTESIAN_POINT('Ctrl Pts',(17.828669100441,-17.0313418722698,3.83441818884811));
#172615=CARTESIAN_POINT('Ctrl Pts',(17.9800398963943,-16.967029414782,3.84307889885775));
#172616=CARTESIAN_POINT('Ctrl Pts',(18.2497877708956,-16.8877893531268,
3.8584682837578));
#172617=CARTESIAN_POINT('Ctrl Pts',(18.3647796710668,-16.8641546683099,
3.86501034560311));
#172618=CARTESIAN_POINT('Ctrl Pts',(18.495320101572,-16.8484493710478,3.87271293993901));
#172619=CARTESIAN_POINT('Ctrl Pts',(18.5095292598403,-16.8468857004034,
3.87355473483307));
#172620=CARTESIAN_POINT('Ctrl Pts',(18.5321672437503,-16.8446262683625,
3.87490168806475));
#172621=CARTESIAN_POINT('Ctrl Pts',(18.5405864386676,-16.8438368902243,
3.87540390262013));
#172622=CARTESIAN_POINT('Ctrl Pts',(18.5554424095455,-16.8425337450981,
3.87629241280931));
#172623=CARTESIAN_POINT('Ctrl Pts',(18.5618772661354,-16.8419989439007,
3.87667804194531));
#172624=CARTESIAN_POINT('Ctrl Pts',(18.575190856144,-16.840953758748,3.87747753669457));
#172625=CARTESIAN_POINT('Ctrl Pts',(18.5820698310345,-16.840447538212,3.87789152842497));
#172626=CARTESIAN_POINT('Ctrl Pts',(18.5997319976758,-16.8392345422098,
3.87895684676922));
#172627=CARTESIAN_POINT('Ctrl Pts',(18.6105182517222,-16.8385767042211,
3.87960970182205));
#172628=CARTESIAN_POINT('Ctrl Pts',(18.6555452815088,-16.8361764448126,
3.88234478481104));
#172629=CARTESIAN_POINT('Ctrl Pts',(18.6898192372429,-16.8351834505981,
3.88445032323934));
#172630=CARTESIAN_POINT('Ctrl Pts',(18.779160516857,-16.834765676957,3.890003538934));
#172631=CARTESIAN_POINT('Ctrl Pts',(18.8342053173157,-16.8366563573999,
3.89348957990565));
#172632=CARTESIAN_POINT('Ctrl Pts',(18.9981747663941,-16.8487026022327,
3.90405710903076));
#172633=CARTESIAN_POINT('Ctrl Pts',(19.1064469602738,-16.8651535644466,
3.91128699468513));
#172634=CARTESIAN_POINT('Ctrl Pts',(19.2565081710211,-16.9000074364045,
3.92146357345564));
#172635=CARTESIAN_POINT('Ctrl Pts',(19.2997315668984,-16.9115009825276,
3.92441189601922));
#172636=CARTESIAN_POINT('Ctrl Pts',(19.3667225176066,-16.9316070516135,
3.92898244550899));
#172637=CARTESIAN_POINT('Ctrl Pts',(19.3907547813336,-16.9392907119383,
3.93062222124833));
#172638=CARTESIAN_POINT('Ctrl Pts',(19.4618700859977,-16.9634373263618,
3.93546477987658));
#172639=CARTESIAN_POINT('Ctrl Pts',(19.5085184738595,-16.9811376585107,
3.9386285377538));
#172640=CARTESIAN_POINT('Ctrl Pts',(19.5617057801968,-17.0034997527569,
3.94218669676189));
#172641=CARTESIAN_POINT('Ctrl Pts',(19.5688931112473,-17.0065685390691,
3.94266645645164));
#172642=CARTESIAN_POINT('Ctrl Pts',(19.5803427049956,-17.0115323295886,
3.94342883181288));
#172643=CARTESIAN_POINT('Ctrl Pts',(19.5846159046973,-17.0134017079738,
3.94371294097046));
#172644=CARTESIAN_POINT('Ctrl Pts',(19.5921676674785,-17.0167351224768,
3.94421423354226));
#172645=CARTESIAN_POINT('Ctrl Pts',(19.5954487270417,-17.0181933956315,
3.94443176466584));
#172646=CARTESIAN_POINT('Ctrl Pts',(19.6023890469679,-17.0212992031604,
3.94489131804331));
#172647=CARTESIAN_POINT('Ctrl Pts',(19.6060473302649,-17.0229487932651,
3.94513321184596));
#172648=CARTESIAN_POINT('Ctrl Pts',(19.6158942044524,-17.0274226732447,
3.94578345080099));
#172649=CARTESIAN_POINT('Ctrl Pts',(19.62207397044,-17.0302664335541,3.94619061589417));
#172650=CARTESIAN_POINT('Ctrl Pts',(19.6524952180077,-17.0444435473644,
3.94819096148223));
#172651=CARTESIAN_POINT('Ctrl Pts',(19.6765352025799,-17.0562065966464,
3.94975909642348));
#172652=CARTESIAN_POINT('Ctrl Pts',(19.7451645107943,-17.0914160505706,
3.95421742905699));
#172653=CARTESIAN_POINT('Ctrl Pts',(19.7891502712375,-17.1160030276241,
3.95705221333874));
#172654=CARTESIAN_POINT('Ctrl Pts',(19.9451769745112,-17.2106796028815,
3.96717298649608));
#172655=CARTESIAN_POINT('Ctrl Pts',(20.0514718891016,-17.2896472539463,
3.97421153969132));
#172656=CARTESIAN_POINT('Ctrl Pts',(20.2269864681888,-17.4475127764653,
3.9871979813182));
#172657=CARTESIAN_POINT('Ctrl Pts',(20.2990259401707,-17.5226014672619,
3.9930368106686));
#172658=CARTESIAN_POINT('Ctrl Pts',(20.3742161951422,-17.6135017929218,
3.99994988500642));
#172659=CARTESIAN_POINT('Ctrl Pts',(20.3830679487324,-17.6244226939959,
4.00077790143366));
#172660=CARTESIAN_POINT('Ctrl Pts',(20.3970261455375,-17.6419987083217,
4.00210691562647));
#172661=CARTESIAN_POINT('Ctrl Pts',(20.4022030298426,-17.6485975321968,
4.00260509243156));
#172662=CARTESIAN_POINT('Ctrl Pts',(20.4112889860191,-17.660321941206,4.00348891078108));
#172663=CARTESIAN_POINT('Ctrl Pts',(20.4152141380485,-17.6654349721844,
4.0038739084213));
#172664=CARTESIAN_POINT('Ctrl Pts',(20.4233084165637,-17.6760791371702,
4.00467452378859));
#172665=CARTESIAN_POINT('Ctrl Pts',(20.4274738667817,-17.6816129584921,
4.00509027964009));
#172666=CARTESIAN_POINT('Ctrl Pts',(20.4381465875191,-17.6959374901244,
4.00616530969077));
#172667=CARTESIAN_POINT('Ctrl Pts',(20.4446129652035,-17.7047582845677,
4.00682616645467));
#172668=CARTESIAN_POINT('Ctrl Pts',(20.4717423031179,-17.7423733032411,
4.00963985230717));
#172669=CARTESIAN_POINT('Ctrl Pts',(20.4917478456482,-17.7716325443616,
4.01181770011623));
#172670=CARTESIAN_POINT('Ctrl Pts',(20.5423376118021,-17.8497629084138,
4.01760878776335));
#172671=CARTESIAN_POINT('Ctrl Pts',(20.5716749686063,-17.8994025921407,
4.02126461491021));
#172672=CARTESIAN_POINT('Ctrl Pts',(20.6748482200605,-18.091464709783,4.03530648712856));
#172673=CARTESIAN_POINT('Ctrl Pts',(20.7344376960959,-18.2409061446823,
4.04607429360625));
#172674=CARTESIAN_POINT('Ctrl Pts',(20.7803435580114,-18.4094395685974,
4.0574348272326));
#172675=CARTESIAN_POINT('Ctrl Pts',(20.7839643612777,-18.4232846601414,
4.05836215204823));
#172676=CARTESIAN_POINT('Ctrl Pts',(20.7900696933786,-18.4476361054248,
4.05998165332226));
#172677=CARTESIAN_POINT('Ctrl Pts',(20.7926147433524,-18.4581266683209,
4.06067560310594));
#172678=CARTESIAN_POINT('Ctrl Pts',(20.8043550495345,-18.5081877484977,
4.06396805562113));
#172679=CARTESIAN_POINT('Ctrl Pts',(20.8124909508737,-18.5480009789565,
4.06652999704423));
#172680=CARTESIAN_POINT('Ctrl Pts',(20.8207425767955,-18.5952807202378,
4.0694869495392));
#172681=CARTESIAN_POINT('Ctrl Pts',(20.8219707990689,-18.6025416015748,
4.06993868969426));
#172682=CARTESIAN_POINT('Ctrl Pts',(20.8239013892064,-18.6143283296685,
4.0706680086335));
#172683=CARTESIAN_POINT('Ctrl Pts',(20.8246269892519,-18.6188502344688,
4.07094685440025));
#172684=CARTESIAN_POINT('Ctrl Pts',(20.8258923568697,-18.6269029003023,
4.07144168781869));
#172685=CARTESIAN_POINT('Ctrl Pts',(20.8264378675351,-18.6304327004786,
4.07165799675415));
#172686=CARTESIAN_POINT('Ctrl Pts',(20.8275920133439,-18.6380280584882,
4.07212215647192));
#172687=CARTESIAN_POINT('Ctrl Pts',(20.8281977392569,-18.6420940014357,
4.07236984145998));
#172688=CARTESIAN_POINT('Ctrl Pts',(20.8298382348117,-18.65333032011,4.0730522100572));
#172689=CARTESIAN_POINT('Ctrl Pts',(20.8308480583633,-18.6605043606289,
4.07348550535171));
#172690=CARTESIAN_POINT('Ctrl Pts',(20.8361967042274,-18.6999691975279,
4.07585673303363));
#172691=CARTESIAN_POINT('Ctrl Pts',(20.8398267298088,-18.7323535666501,
4.07775711901633));
#172692=CARTESIAN_POINT('Ctrl Pts',(20.8570892017347,-18.92681727768,4.08896587802496));
#172693=CARTESIAN_POINT('Ctrl Pts',(20.8527546651832,-19.0899580453236,
4.09756266631738));
#172694=CARTESIAN_POINT('Ctrl Pts',(20.8132771506168,-19.3666607797021,
4.1128641864491));
#172695=CARTESIAN_POINT('Ctrl Pts',(20.7872343545411,-19.4807347696848,
4.11938601378332));
#172696=CARTESIAN_POINT('Ctrl Pts',(20.7475989285466,-19.6056914830379,
4.12706583117076));
#172697=CARTESIAN_POINT('Ctrl Pts',(20.7431406986708,-19.6192681905171,
4.12790733665854));
#172698=CARTESIAN_POINT('Ctrl Pts',(20.7358265267352,-19.6408040641056,
4.12925391330786));
#172699=CARTESIAN_POINT('Ctrl Pts',(20.7330597085465,-19.6487931977078,
4.12975604329215));
#172700=CARTESIAN_POINT('Ctrl Pts',(20.7280956111988,-19.6628539822056,
4.130644454966));
#172701=CARTESIAN_POINT('Ctrl Pts',(20.7259182590846,-19.6689325898016,
4.13103007063195));
#172702=CARTESIAN_POINT('Ctrl Pts',(20.7213572721845,-19.6814845150261,
4.131829587642));
#172703=CARTESIAN_POINT('Ctrl Pts',(20.7189697402013,-19.6879563259464,
4.1322436153506));
#172704=CARTESIAN_POINT('Ctrl Pts',(20.7127600158151,-19.7045387921159,
4.13330913198197));
#172705=CARTESIAN_POINT('Ctrl Pts',(20.7088919767256,-19.7146319605857,
4.1339621504423));
#172706=CARTESIAN_POINT('Ctrl Pts',(20.6924245296528,-19.7566362010405,
4.13669881683496));
#172707=CARTESIAN_POINT('Ctrl Pts',(20.6791282008865,-19.7882667756943,
4.13880580902997));
#172708=CARTESIAN_POINT('Ctrl Pts',(20.6424846364209,-19.8698304339781,
4.14436377314599));
#172709=CARTESIAN_POINT('Ctrl Pts',(20.6179467356701,-19.9191970786531,
4.14785319061943));
#172710=CARTESIAN_POINT('Ctrl Pts',(20.5390317512022,-20.0635385596571,
4.15842720592655));
#172711=CARTESIAN_POINT('Ctrl Pts',(20.4791925194379,-20.15531093108,4.16566017969358));
#172712=CARTESIAN_POINT('Ctrl Pts',(20.3828537962609,-20.2806620365107,
4.176103493032));
#172713=CARTESIAN_POINT('Ctrl Pts',(20.3518464901503,-20.3182483759927,
4.17931472136264));
#172714=CARTESIAN_POINT('Ctrl Pts',(20.3080707575026,-20.3677299911857,
4.18362416080086));
#172715=CARTESIAN_POINT('Ctrl Pts',(20.2964123899318,-20.3805859108204,
4.18475165787128));
#172716=CARTESIAN_POINT('Ctrl Pts',(20.2482575777891,-20.4323925099416,
4.18932303072838));
#172717=CARTESIAN_POINT('Ctrl Pts',(20.2104490714907,-20.4701031496099,
4.19271619582484));
#172718=CARTESIAN_POINT('Ctrl Pts',(20.1648482747888,-20.5122686586665,
4.19654748053733));
#172719=CARTESIAN_POINT('Ctrl Pts',(20.1584077585188,-20.5181505726358,
4.19708280915994));
#172720=CARTESIAN_POINT('Ctrl Pts',(20.1486016335192,-20.5269956574417,
4.1978889126663));
#172721=CARTESIAN_POINT('Ctrl Pts',(20.1452627515513,-20.5299881334962,
4.19816182552491));
#172722=CARTESIAN_POINT('Ctrl Pts',(20.1392528137062,-20.5353402133521,
4.19865023694286));
#172723=CARTESIAN_POINT('Ctrl Pts',(20.1365852956949,-20.5377036893859,
4.19886602378302));
#172724=CARTESIAN_POINT('Ctrl Pts',(20.1307765613152,-20.5428242220714,
4.19933375530113));
#172725=CARTESIAN_POINT('Ctrl Pts',(20.1276331552509,-20.5455787075157,
4.19958550908801));
#172726=CARTESIAN_POINT('Ctrl Pts',(20.1187818434445,-20.5532886629269,
4.20029066479879));
#172727=CARTESIAN_POINT('Ctrl Pts',(20.1130554585783,-20.5582229552659,
4.20074252173185));
#172728=CARTESIAN_POINT('Ctrl Pts',(20.0786891501913,-20.5875163356939,
4.20342930969765));
#172729=CARTESIAN_POINT('Ctrl Pts',(20.0494289484576,-20.6111412445241,
4.20561392778844));
#172730=CARTESIAN_POINT('Ctrl Pts',(19.9511263783463,-20.6862750047007,
4.21267968183811));
#172731=CARTESIAN_POINT('Ctrl Pts',(19.8795663476027,-20.7343542018459,
4.21739797804719));
#172732=CARTESIAN_POINT('Ctrl Pts',(19.652829988649,-20.8673792323252,4.23170432042636));
#172733=CARTESIAN_POINT('Ctrl Pts',(19.4898086759238,-20.9373646409992,
4.24120007847877));
#172734=CARTESIAN_POINT('Ctrl Pts',(19.2979887004385,-20.9926200220358,
4.25280076814476));
#172735=CARTESIAN_POINT('Ctrl Pts',(19.2758844677203,-20.9986007163114,
4.25414235637142));
#172736=CARTESIAN_POINT('Ctrl Pts',(19.2444489369933,-21.0065611990252,
4.25605878434435));
#172737=CARTESIAN_POINT('Ctrl Pts',(19.2351941095054,-21.0088384228955,
4.25662402395593));
#172738=CARTESIAN_POINT('Ctrl Pts',(19.2201234937752,-21.0124389142055,
4.25754625447383));
#172739=CARTESIAN_POINT('Ctrl Pts',(19.2143168695668,-21.0138002507666,
4.25790201526899));
#172740=CARTESIAN_POINT('Ctrl Pts',(19.2021436046721,-21.0166000019803,
4.25864878230591));
#172741=CARTESIAN_POINT('Ctrl Pts',(19.1957759178932,-21.0180335435189,
4.25903994087415));
#172742=CARTESIAN_POINT('Ctrl Pts',(19.1805993514443,-21.0213765392341,
4.25997353223949));
#172743=CARTESIAN_POINT('Ctrl Pts',(19.1717847600478,-21.0232592164636,
4.26051681712549));
#172744=CARTESIAN_POINT('Ctrl Pts',(19.1419896847806,-21.029424351108,4.26235692391388));
#172745=CARTESIAN_POINT('Ctrl Pts',(19.1209568613373,-21.0334446550569,
4.26366207199765));
#172746=CARTESIAN_POINT('Ctrl Pts',(19.0707415851066,-21.0422556128637,
4.26679375978029));
#172747=CARTESIAN_POINT('Ctrl Pts',(19.0415132385426,-21.0467550916538,
4.26862915598807));
#172748=CARTESIAN_POINT('Ctrl Pts',(18.843318555189,-21.0730283001473,4.28116187296321));
#172749=CARTESIAN_POINT('Ctrl Pts',(18.6723714835105,-21.0749450630205,
4.29247109123198));
#172750=CARTESIAN_POINT('Ctrl Pts',(18.4039127858904,-21.0454860698564,
4.3102647913417));
#172751=CARTESIAN_POINT('Ctrl Pts',(18.3056266028396,-21.0276065267998,
4.31676753280609));
#172752=CARTESIAN_POINT('Ctrl Pts',(18.19956691186,-21.0004541132151,4.3235317165698));
#172753=CARTESIAN_POINT('Ctrl Pts',(18.1901919011292,-20.9979852735181,
4.32412736630247));
#172754=CARTESIAN_POINT('Ctrl Pts',(18.1763750908517,-20.9942450389934,
4.32500154581603));
#172755=CARTESIAN_POINT('Ctrl Pts',(18.1719201170092,-20.9930234062026,
4.32528284120623));
#172756=CARTESIAN_POINT('Ctrl Pts',(18.1640238970266,-20.9908303086036,
4.3257803710753));
#172757=CARTESIAN_POINT('Ctrl Pts',(18.1605810812025,-20.989864698523,4.32599694041291));
#172758=CARTESIAN_POINT('Ctrl Pts',(18.1532101339695,-20.9877772028319,
4.32645983097572));
#172759=CARTESIAN_POINT('Ctrl Pts',(18.14928280938,-20.9866526720047,4.32670599599692));
#172760=CARTESIAN_POINT('Ctrl Pts',(18.1385117459141,-20.983534776636,4.32737990272118));
#172761=CARTESIAN_POINT('Ctrl Pts',(18.1316747085127,-20.9815181832054,
4.32780631237714));
#172762=CARTESIAN_POINT('Ctrl Pts',(18.0952340843999,-20.9705696040853,
4.33007240364837));
#172763=CARTESIAN_POINT('Ctrl Pts',(18.0658170093122,-20.9610238573582,
4.33187835544342));
#172764=CARTESIAN_POINT('Ctrl Pts',(17.9774236090361,-20.9301839300038,
4.33726331477463));
#172765=CARTESIAN_POINT('Ctrl Pts',(17.9191714013096,-20.9069104837852,
4.34075559236385));
#172766=CARTESIAN_POINT('Ctrl Pts',(17.7219706492996,-20.8177737363914,
4.35264919877123));
#172767=CARTESIAN_POINT('Ctrl Pts',(17.5892223540265,-20.7394002591372,
4.36081661047618));
#172768=CARTESIAN_POINT('Ctrl Pts',(17.4622379180975,-20.6444342844427,
4.36970909216085));
#172769=CARTESIAN_POINT('Ctrl Pts',(17.4583575640986,-20.6415114605778,
4.36998191255556));
#172770=CARTESIAN_POINT('Ctrl Pts',(17.4040558575116,-20.6003157184154,
4.37381531857891));
#172771=CARTESIAN_POINT('Ctrl Pts',(17.3553698866704,-20.5598165391312,
4.3774424392865));
#172772=CARTESIAN_POINT('Ctrl Pts',(17.2993257549232,-20.5087772114836,
4.38189394341832));
#172773=CARTESIAN_POINT('Ctrl Pts',(17.2901522188873,-20.500272925101,4.38263190214923));
#172774=CARTESIAN_POINT('Ctrl Pts',(17.2752274191951,-20.4861889565102,
4.3838482227587));
#172775=CARTESIAN_POINT('Ctrl Pts',(17.2694314319325,-20.4806569607065,
4.38432453625511));
#172776=CARTESIAN_POINT('Ctrl Pts',(17.2590770460138,-20.4706612465413,
4.38518268437635));
#172777=CARTESIAN_POINT('Ctrl Pts',(17.2545071364174,-20.4662095519354,
4.38556399268506));
#172778=CARTESIAN_POINT('Ctrl Pts',(17.2456932590751,-20.4575456811477,
4.38630443929746));
#172779=CARTESIAN_POINT('Ctrl Pts',(17.2414468729001,-20.4533360432453,
4.38666346397012));
#172780=CARTESIAN_POINT('Ctrl Pts',(17.2299422995142,-20.4418339820608,
4.38764244842814));
#172781=CARTESIAN_POINT('Ctrl Pts',(17.2227194195755,-20.434506614445,4.38826395895046));
#172782=CARTESIAN_POINT('Ctrl Pts',(17.1934248661666,-20.404351715827,4.39081324186662));
#172783=CARTESIAN_POINT('Ctrl Pts',(17.1718156123648,-20.3810825786974,
4.39276089049446));
#172784=CARTESIAN_POINT('Ctrl Pts',(17.1176145239884,-20.3200193095613,
4.39782554201291));
#172785=CARTESIAN_POINT('Ctrl Pts',(17.0858223367537,-20.2815445116243,
4.40097335656107));
#172786=CARTESIAN_POINT('Ctrl Pts',(17.0102400644393,-20.1831938779723,
4.40891138223178));
#172787=CARTESIAN_POINT('Ctrl Pts',(16.9681822759228,-20.1220739429574,
4.41375216312812));
#172788=CARTESIAN_POINT('Ctrl Pts',(16.8493472984656,-19.9283332935157,
4.42872202418659));
#172789=CARTESIAN_POINT('Ctrl Pts',(16.7836721142417,-19.7894782272955,
4.43897491950335));
#172790=CARTESIAN_POINT('Ctrl Pts',(16.7284957728217,-19.6301449193315,
4.44949009207163));
#172791=CARTESIAN_POINT('Ctrl Pts',(16.7235995346047,-19.6154890635135,
4.45044585903614));
#172792=CARTESIAN_POINT('Ctrl Pts',(16.7171006642882,-19.5953033326114,
4.4517453404905));
#172793=CARTESIAN_POINT('Ctrl Pts',(16.7153596043772,-19.5898189892765,
4.45209669915286));
#172794=CARTESIAN_POINT('Ctrl Pts',(16.7126241720105,-19.5810789688052,
4.45265385178579));
#172795=CARTESIAN_POINT('Ctrl Pts',(16.7116152688895,-19.5778279210169,
4.45286048602846));
#172796=CARTESIAN_POINT('Ctrl Pts',(16.7095441627949,-19.5710967633095,
4.45328702903049));
#172797=CARTESIAN_POINT('Ctrl Pts',(16.7084830894302,-19.5676163450457,
4.4535068657369));
#172798=CARTESIAN_POINT('Ctrl Pts',(16.7059703329421,-19.5592974456252,
4.45403065433402));
#172799=CARTESIAN_POINT('Ctrl Pts',(16.7045269733107,-19.5544564325111,
4.45433412059053));
#172800=CARTESIAN_POINT('Ctrl Pts',(16.6996912606082,-19.5380229049513,
4.45535988124939));
#172801=CARTESIAN_POINT('Ctrl Pts',(16.696380723361,-19.5264062944156,4.45607756586052));
#172802=CARTESIAN_POINT('Ctrl Pts',(16.6886498163706,-19.4983705029819,
4.45779325489078));
#172803=CARTESIAN_POINT('Ctrl Pts',(16.6843274150554,-19.4819249306869,
4.45878621140754));
#172804=CARTESIAN_POINT('Ctrl Pts',(16.6687721240632,-19.4197012718665,
4.46249872608696));
#172805=CARTESIAN_POINT('Ctrl Pts',(16.6588703556768,-19.3736019354585,
4.46515906019934));
#172806=CARTESIAN_POINT('Ctrl Pts',(16.6283221911304,-19.2039715288572,
4.47474467089376));
#172807=CARTESIAN_POINT('Ctrl Pts',(16.6171065839709,-19.0790096628014,
4.48142927135385));
#172808=CARTESIAN_POINT('Ctrl Pts',(16.6170007560322,-18.9537891450234,
4.48828854762057));
#172809=CARTESIAN_POINT('Ctrl Pts',(16.6170007544017,-18.9537872147055,
4.48828865335871));
#172810=CARTESIAN_POINT('Ctrl Pts',(16.6169304739052,-18.8705382588802,
4.49284883024313));
#172811=CARTESIAN_POINT('Ctrl Pts',(16.6217706707422,-18.7873622863883,
4.49747291987405));
#172812=CARTESIAN_POINT('Ctrl Pts',(16.6354867574308,-18.6707551618226,
4.5041975533329));
#172813=CARTESIAN_POINT('Ctrl Pts',(16.6402991570916,-18.6369236936205,
4.50617710222748));
#172814=CARTESIAN_POINT('Ctrl Pts',(16.6476157990064,-18.5931199034441,
4.50878346471332));
#172815=CARTESIAN_POINT('Ctrl Pts',(16.6493769494046,-18.5830275223217,
4.50938696765868));
#172816=CARTESIAN_POINT('Ctrl Pts',(16.6524781169082,-18.5659874210792,
4.51041117473668));
#172817=CARTESIAN_POINT('Ctrl Pts',(16.6537798486759,-18.5590328499048,
4.51083066560809));
#172818=CARTESIAN_POINT('Ctrl Pts',(16.6564245881202,-18.5452846648746,
4.51166293212674));
#172819=CARTESIAN_POINT('Ctrl Pts',(16.6577661161461,-18.5384908542017,
4.51207565605965));
#172820=CARTESIAN_POINT('Ctrl Pts',(16.6604207784662,-18.5253856910209,
4.51287464746878));
#172821=CARTESIAN_POINT('Ctrl Pts',(16.6617294562935,-18.5190735063975,
4.51326076834749));
#172822=CARTESIAN_POINT('Ctrl Pts',(16.6648077475785,-18.5045597021983,
4.51415158331865));
#172823=CARTESIAN_POINT('Ctrl Pts',(16.6665973215928,-18.4963624689217,
4.51465691248745));
#172824=CARTESIAN_POINT('Ctrl Pts',(16.6715178729829,-18.4744495882456,
4.51601377176292));
#172825=CARTESIAN_POINT('Ctrl Pts',(16.6747368802982,-18.4607543294126,
4.51686811537757));
#172826=CARTESIAN_POINT('Ctrl Pts',(16.6964948318064,-18.3721592143423,
4.52243687221738));
#172827=CARTESIAN_POINT('Ctrl Pts',(16.7189735909982,-18.2983161719576,
4.52727680159809));
#172828=CARTESIAN_POINT('Ctrl Pts',(16.7454193964829,-18.2258896892926,
4.53222340662745));
#172829=CARTESIAN_POINT('Origin',(18.734,-18.952,0.));
#172830=CARTESIAN_POINT('',(16.7454193466937,-18.2258898256491,5.55626851740655));
#172831=CARTESIAN_POINT('',(16.7454193844609,-18.2258897222169,5.33540091855302));
#172832=CARTESIAN_POINT('',(16.7454193692319,-18.2258897639242,0.));
#172833=CARTESIAN_POINT('Ctrl Pts',(16.7454193466937,-18.2258898256491,
5.55626851740655));
#172834=CARTESIAN_POINT('Ctrl Pts',(16.7359008843311,-18.2519578119853,
5.55474535788985));
#172835=CARTESIAN_POINT('Ctrl Pts',(16.7268931576281,-18.2782180124468,
5.55321402945697));
#172836=CARTESIAN_POINT('Ctrl Pts',(16.6925866539401,-18.3850361381322,
5.54697988874858));
#172837=CARTESIAN_POINT('Ctrl Pts',(16.6716050349134,-18.4668803814372,
5.54218747913845));
#172838=CARTESIAN_POINT('Ctrl Pts',(16.6528673380296,-18.5636990438631,
5.53639853261415));
#172839=CARTESIAN_POINT('Ctrl Pts',(16.6503087149706,-18.5776720646127,
5.53556032075485));
#172840=CARTESIAN_POINT('Ctrl Pts',(16.6465902594023,-18.5991998131029,
5.53426430419031));
#172841=CARTESIAN_POINT('Ctrl Pts',(16.645330360663,-18.6067370098265,5.53380968308545));
#172842=CARTESIAN_POINT('Ctrl Pts',(16.643106864088,-18.6204965478617,5.53297810679902));
#172843=CARTESIAN_POINT('Ctrl Pts',(16.642130161454,-18.6267167052547,5.53260157251945));
#172844=CARTESIAN_POINT('Ctrl Pts',(16.6400580228059,-18.6403085853967,
5.53177742293717));
#172845=CARTESIAN_POINT('Ctrl Pts',(16.6389737391432,-18.6476819001443,
5.53132945929608));
#172846=CARTESIAN_POINT('Ctrl Pts',(16.6361094454989,-18.6679007286344,
5.530098589618));
#172847=CARTESIAN_POINT('Ctrl Pts',(16.6344085221732,-18.6807569555613,
5.52931319511429));
#172848=CARTESIAN_POINT('Ctrl Pts',(16.6263685192506,-18.7461410985298,
5.52530435191713));
#172849=CARTESIAN_POINT('Ctrl Pts',(16.6218825840024,-18.7988739559501,
5.52202307361011));
#172850=CARTESIAN_POINT('Ctrl Pts',(16.6177663610352,-18.885670091598,5.51653981045079));
#172851=CARTESIAN_POINT('Ctrl Pts',(16.6169742107339,-18.91965658388,5.51437225302693));
#172852=CARTESIAN_POINT('Ctrl Pts',(16.6171022078418,-19.0842687455959,
5.5037810395224));
#172853=CARTESIAN_POINT('Ctrl Pts',(16.6292932821579,-19.2145944755365,
5.49508949971731));
#172854=CARTESIAN_POINT('Ctrl Pts',(16.6709615190644,-19.4363469018122,
5.48023959087602));
#172855=CARTESIAN_POINT('Ctrl Pts',(16.6947819163944,-19.5284664524788,
5.47405980222472));
#172856=CARTESIAN_POINT('Ctrl Pts',(16.727765752138,-19.6278749492191,5.46758873518461));
#172857=CARTESIAN_POINT('Ctrl Pts',(16.7308789343071,-19.6370465740627,
5.46699364833627));
#172858=CARTESIAN_POINT('Ctrl Pts',(16.7355692047997,-19.6505590019216,
5.46612013419701));
#172859=CARTESIAN_POINT('Ctrl Pts',(16.7370976766823,-19.6549163779793,
5.46583894724034));
#172860=CARTESIAN_POINT('Ctrl Pts',(16.7398349366883,-19.6626387860223,
5.46534153720036));
#172861=CARTESIAN_POINT('Ctrl Pts',(16.7410380035872,-19.6660057881174,
5.465124979859));
#172862=CARTESIAN_POINT('Ctrl Pts',(16.7436342810792,-19.6732142552974,
5.46466203532028));
#172863=CARTESIAN_POINT('Ctrl Pts',(16.7450300811399,-19.6770547287055,
5.46441580474307));
#172864=CARTESIAN_POINT('Ctrl Pts',(16.7488929553554,-19.6875881335771,
5.46374153367509));
#172865=CARTESIAN_POINT('Ctrl Pts',(16.7513827766128,-19.6942727462213,
5.46331482763278));
#172866=CARTESIAN_POINT('Ctrl Pts',(16.7648702439157,-19.7299315152197,
5.46104432982681));
#172867=CARTESIAN_POINT('Ctrl Pts',(16.7764699573688,-19.758675770873,5.45923442348496));
#172868=CARTESIAN_POINT('Ctrl Pts',(16.8532264206235,-19.9374620610696,
5.44804383693206));
#172869=CARTESIAN_POINT('Ctrl Pts',(16.9349648030108,-20.07979849345,5.4393986993646));
#172870=CARTESIAN_POINT('Ctrl Pts',(17.1022876526277,-20.3059020269329,
5.42400418916545));
#172871=CARTESIAN_POINT('Ctrl Pts',(17.1800410560598,-20.3944777785986,
5.41743777573114));
#172872=CARTESIAN_POINT('Ctrl Pts',(17.2750386715052,-20.486055197147,5.40970777271542));
#172873=CARTESIAN_POINT('Ctrl Pts',(17.2854344387419,-20.4958754178144,
5.40886564583278));
#172874=CARTESIAN_POINT('Ctrl Pts',(17.3021355842578,-20.5113347393207,
5.40751826057675));
#172875=CARTESIAN_POINT('Ctrl Pts',(17.3083767585881,-20.5170427804698,
5.40701594897468));
#172876=CARTESIAN_POINT('Ctrl Pts',(17.3194429387323,-20.527042544702,5.4061273256713));
#172877=CARTESIAN_POINT('Ctrl Pts',(17.324253717047,-20.531349902168,5.40574168101176));
#172878=CARTESIAN_POINT('Ctrl Pts',(17.3342433771475,-20.5402121912422,
5.40494221158013));
#172879=CARTESIAN_POINT('Ctrl Pts',(17.339424956335,-20.5447639540953,5.4045282609742));
#172880=CARTESIAN_POINT('Ctrl Pts',(17.3527797536973,-20.5563803605167,
5.40346316950663));
#172881=CARTESIAN_POINT('Ctrl Pts',(17.3609849003692,-20.5634078439113,
5.40281050146319));
#172882=CARTESIAN_POINT('Ctrl Pts',(17.3954326820626,-20.5924573056214,
5.40007723009742));
#172883=CARTESIAN_POINT('Ctrl Pts',(17.4221529410106,-20.613902438357,5.39797335489242));
#172884=CARTESIAN_POINT('Ctrl Pts',(17.4930984155857,-20.6680645208865,
5.39242557024259));
#172885=CARTESIAN_POINT('Ctrl Pts',(17.5380970725674,-20.6997212459683,
5.38894339058952));
#172886=CARTESIAN_POINT('Ctrl Pts',(17.6611867388643,-20.7793343759979,
5.37952162449786));
#172887=CARTESIAN_POINT('Ctrl Pts',(17.7412415107427,-20.8240330014683,
5.37349486871033));
#172888=CARTESIAN_POINT('Ctrl Pts',(17.8723921801402,-20.8864770904454,
5.36389706536462));
#172889=CARTESIAN_POINT('Ctrl Pts',(17.921712036845,-20.9076988725713,5.36034702183442));
#172890=CARTESIAN_POINT('Ctrl Pts',(18.0061637171794,-20.9402910298159,
5.35441155329808));
#172891=CARTESIAN_POINT('Ctrl Pts',(18.0408836779819,-20.9526591030056,
5.35201099068368));
#172892=CARTESIAN_POINT('Ctrl Pts',(18.1208910951545,-20.9788266329332,
5.34659306904659));
#172893=CARTESIAN_POINT('Ctrl Pts',(18.1663567646846,-20.9920271172026,
5.34359566530302));
#172894=CARTESIAN_POINT('Ctrl Pts',(18.2196964179984,-21.0055920172991,
5.34020231494323));
#172895=CARTESIAN_POINT('Ctrl Pts',(18.2271729697419,-21.0074500026783,
5.33972945975241));
#172896=CARTESIAN_POINT('Ctrl Pts',(18.2391605365535,-21.0103596277329,
5.33897594524377));
#172897=CARTESIAN_POINT('Ctrl Pts',(18.2436650691388,-21.011437328054,5.33869384535696));
#172898=CARTESIAN_POINT('Ctrl Pts',(18.2516635997707,-21.0133232297586,
5.33819483045165));
#172899=CARTESIAN_POINT('Ctrl Pts',(18.2551561565076,-21.0141373462514,
5.33797757859747));
#172900=CARTESIAN_POINT('Ctrl Pts',(18.262579167711,-21.015847777812,5.33751721362111));
#172901=CARTESIAN_POINT('Ctrl Pts',(18.2665101097136,-21.0167417403152,
5.3372742361178));
#172902=CARTESIAN_POINT('Ctrl Pts',(18.2771614480846,-21.0191320566201,
5.33661800488184));
#172903=CARTESIAN_POINT('Ctrl Pts',(18.2838866969936,-21.020606878905,5.33620596894611));
#172904=CARTESIAN_POINT('Ctrl Pts',(18.3177561661862,-21.0278613330994,
5.3341419411297));
#172905=CARTESIAN_POINT('Ctrl Pts',(18.3450063639415,-21.0331399092261,
5.33251695090472));
#172906=CARTESIAN_POINT('Ctrl Pts',(18.4247475690468,-21.0469652849544,
5.32784471454025));
#172907=CARTESIAN_POINT('Ctrl Pts',(18.4774685848287,-21.0540725528601,
5.3248594438555));
#172908=CARTESIAN_POINT('Ctrl Pts',(18.6705343316279,-21.0727264684781,
5.31412794462035));
#172909=CARTESIAN_POINT('Ctrl Pts',(18.8116660994787,-21.0722544315329,
5.30664406807786));
#172910=CARTESIAN_POINT('Ctrl Pts',(19.0430844231071,-21.0483287866107,
5.29377488274038));
#172911=CARTESIAN_POINT('Ctrl Pts',(19.1337369952539,-21.0329456755309,
5.28858388886549));
#172912=CARTESIAN_POINT('Ctrl Pts',(19.2364887274002,-21.0085465017107,
5.28239265087972));
#172913=CARTESIAN_POINT('Ctrl Pts',(19.2498483281825,-21.00523620751,5.28158172383808));
#172914=CARTESIAN_POINT('Ctrl Pts',(19.2712120751727,-20.9997209514359,
5.28027498800694));
#172915=CARTESIAN_POINT('Ctrl Pts',(19.2792373173305,-20.9975987322678,
5.27978185124187));
#172916=CARTESIAN_POINT('Ctrl Pts',(19.2934588752124,-20.9937483061839,
5.27890385386484));
#172917=CARTESIAN_POINT('Ctrl Pts',(19.2996602182366,-20.9920389444697,
5.27851960907695));
#172918=CARTESIAN_POINT('Ctrl Pts',(19.3125592840503,-20.9884200598194,
5.27771741969674));
#172919=CARTESIAN_POINT('Ctrl Pts',(19.3192555582502,-20.9865056979348,
5.27729932140178));
#172920=CARTESIAN_POINT('Ctrl Pts',(19.3366093753671,-20.9814517437655,
5.27621142450831));
#172921=CARTESIAN_POINT('Ctrl Pts',(19.3472517637493,-20.9782612631248,
5.2755399706083));
#172922=CARTESIAN_POINT('Ctrl Pts',(19.3932524252594,-20.9640751335714,
5.27261871195812));
#172923=CARTESIAN_POINT('Ctrl Pts',(19.4283421815413,-20.9522371776136,
5.27034144501515));
#172924=CARTESIAN_POINT('Ctrl Pts',(19.5206273164225,-20.9183827158465,
5.26421754509036));
#172925=CARTESIAN_POINT('Ctrl Pts',(19.5772047983738,-20.8947938863392,
5.26032198678025));
#172926=CARTESIAN_POINT('Ctrl Pts',(19.7734805152882,-20.8027709938382,
5.24632186742231));
#172927=CARTESIAN_POINT('Ctrl Pts',(19.9065686253226,-20.7214490469248,
5.23588573570889));
#172928=CARTESIAN_POINT('Ctrl Pts',(20.04189546632,-20.6167349084246,5.22476105877163));
#172929=CARTESIAN_POINT('Ctrl Pts',(20.0541401252136,-20.6070416715196,
5.22374985132899));
#172930=CARTESIAN_POINT('Ctrl Pts',(20.1040988825323,-20.566585597837,5.21960830584544));
#172931=CARTESIAN_POINT('Ctrl Pts',(20.1408570825245,-20.5346596479578,
5.21652329509552));
#172932=CARTESIAN_POINT('Ctrl Pts',(20.1821676888973,-20.4962019386202,
5.21304298154817));
#172933=CARTESIAN_POINT('Ctrl Pts',(20.1878214614105,-20.4908802568677,
5.21256637217816));
#172934=CARTESIAN_POINT('Ctrl Pts',(20.1968138283211,-20.4823222927788,
5.21180803834416));
#172935=CARTESIAN_POINT('Ctrl Pts',(20.2001711992745,-20.479105966026,5.21152484464288));
#172936=CARTESIAN_POINT('Ctrl Pts',(20.2061010862889,-20.4733876130133,
5.21102459145544));
#172937=CARTESIAN_POINT('Ctrl Pts',(20.2086778691496,-20.4708900751069,
5.21080718921328));
#172938=CARTESIAN_POINT('Ctrl Pts',(20.2141286873532,-20.4655799413635,
5.21034727370704));
#172939=CARTESIAN_POINT('Ctrl Pts',(20.2170010572892,-20.4627657113937,
5.21010489213194));
#172940=CARTESIAN_POINT('Ctrl Pts',(20.2247372779883,-20.4551427570659,
5.20945195697488));
#172941=CARTESIAN_POINT('Ctrl Pts',(20.2295859203568,-20.4503185702149,
5.20904260037014));
#172942=CARTESIAN_POINT('Ctrl Pts',(20.253601038531,-20.426191851873,5.20701388280868));
#172943=CARTESIAN_POINT('Ctrl Pts',(20.2724185746045,-20.4065437015529,
5.20542042921281));
#172944=CARTESIAN_POINT('Ctrl Pts',(20.3258253031997,-20.3485832464852,
5.2008674013323));
#172945=CARTESIAN_POINT('Ctrl Pts',(20.3594002848401,-20.3093603769208,
5.1979660963545));
#172946=CARTESIAN_POINT('Ctrl Pts',(20.477228516741,-20.1610617134911,5.18747332338905));
#172947=CARTESIAN_POINT('Ctrl Pts',(20.5522105038521,-20.0450639829885,
5.18014387401597));
#172948=CARTESIAN_POINT('Ctrl Pts',(20.6300376601681,-19.8942053634468,
5.17077621990492));
#172949=CARTESIAN_POINT('Ctrl Pts',(20.6440406809721,-19.8654846740376,
5.1690008260937));
#172950=CARTESIAN_POINT('Ctrl Pts',(20.6853895917279,-19.7755652799806,
5.16344810184575));
#172951=CARTESIAN_POINT('Ctrl Pts',(20.7104811944482,-19.7133815672481,
5.15961475188325));
#172952=CARTESIAN_POINT('Ctrl Pts',(20.7367727534823,-19.6381136565477,
5.15493406682916));
#172953=CARTESIAN_POINT('Ctrl Pts',(20.7408572017516,-19.6260732994402,
5.1541841638845));
#172954=CARTESIAN_POINT('Ctrl Pts',(20.7473579955751,-19.6063269735402,
5.15295213084223));
#172955=CARTESIAN_POINT('Ctrl Pts',(20.749839177489,-19.598642570813,5.15247214119126));
#172956=CARTESIAN_POINT('Ctrl Pts',(20.7542037330234,-19.5848559546031,
5.15160995480767));
#172957=CARTESIAN_POINT('Ctrl Pts',(20.7561035826163,-19.5787590302404,
5.15122830503331));
#172958=CARTESIAN_POINT('Ctrl Pts',(20.7600734600284,-19.5658131049891,
5.15041712365904));
#172959=CARTESIAN_POINT('Ctrl Pts',(20.7621364064564,-19.5589620318744,
5.14998736548389));
#172960=CARTESIAN_POINT('Ctrl Pts',(20.7675575871534,-19.5406219616332,
5.14883558624048));
#172961=CARTESIAN_POINT('Ctrl Pts',(20.7708531414546,-19.5291148455117,
5.1481115306973));
#172962=CARTESIAN_POINT('Ctrl Pts',(20.7863447022556,-19.4732367385839,
5.14458835558003));
#172963=CARTESIAN_POINT('Ctrl Pts',(20.7971886090947,-19.4285068308974,
5.14174580910474));
#172964=CARTESIAN_POINT('Ctrl Pts',(20.8410865586169,-19.2176390033274,
5.12823209825699));
#172965=CARTESIAN_POINT('Ctrl Pts',(20.8555768467132,-19.0482924557364,
5.11698566285067));
#172966=CARTESIAN_POINT('Ctrl Pts',(20.8463190488305,-18.7797321213914,
5.09928230616555));
#172967=CARTESIAN_POINT('Ctrl Pts',(20.8359029716536,-18.680749975873,5.092804795141));
#172968=CARTESIAN_POINT('Ctrl Pts',(20.816877115971,-18.5733102788523,5.08606340077225));
#172969=CARTESIAN_POINT('Ctrl Pts',(20.8151210687593,-18.5637757213809,
5.0854677334217));
#172970=CARTESIAN_POINT('Ctrl Pts',(20.8124316394239,-18.5497161955159,
5.08459353305305));
#172971=CARTESIAN_POINT('Ctrl Pts',(20.8115488734488,-18.5451818361064,
5.08431223423984));
#172972=CARTESIAN_POINT('Ctrl Pts',(20.8099564858598,-18.5371428509674,
5.08381470055339));
#172973=CARTESIAN_POINT('Ctrl Pts',(20.8092528208595,-18.5336371007351,
5.08359813080258));
#172974=CARTESIAN_POINT('Ctrl Pts',(20.8077262056343,-18.5261299354911,
5.08313524182846));
#172975=CARTESIAN_POINT('Ctrl Pts',(20.806900557178,-18.522129125807,5.08288907879628));
#172976=CARTESIAN_POINT('Ctrl Pts',(20.8046024912724,-18.5111540741109,
5.08221518325148));
#172977=CARTESIAN_POINT('Ctrl Pts',(20.8031064076511,-18.5041847653949,
5.08178878271177));
#172978=CARTESIAN_POINT('Ctrl Pts',(20.7949329799469,-18.4670255047476,
5.07952282752548));
#172979=CARTESIAN_POINT('Ctrl Pts',(20.7876296646545,-18.4369753051609,
5.07771699789486));
#172980=CARTESIAN_POINT('Ctrl Pts',(20.7635348963703,-18.3465194026107,
5.07233253738531));
#172981=CARTESIAN_POINT('Ctrl Pts',(20.7447157619216,-18.2866865983345,
5.06884061755312));
#172982=CARTESIAN_POINT('Ctrl Pts',(20.6772851160064,-18.1014716602466,
5.05800781631651));
#172983=CARTESIAN_POINT('Ctrl Pts',(20.6193796952157,-17.9798376645672,
5.05083994676616));
#172984=CARTESIAN_POINT('Ctrl Pts',(20.529375547633,-17.829511712847,5.04111629893205));
#172985=CARTESIAN_POINT('Ctrl Pts',(20.5074124473629,-17.7951243117778,
5.03882943063877));
#172986=CARTESIAN_POINT('Ctrl Pts',(20.4571198046639,-17.7211823126013,
5.03374715354906));
#172987=CARTESIAN_POINT('Ctrl Pts',(20.4283934804564,-17.6819274665458,
5.03093987799765));
#172988=CARTESIAN_POINT('Ctrl Pts',(20.3905520674963,-17.6337878923138,
5.02733863546636));
#172989=CARTESIAN_POINT('Ctrl Pts',(20.3826733027,-17.6239471984142,5.02659380992691));
#172990=CARTESIAN_POINT('Ctrl Pts',(20.370050220488,-17.6084662327259,5.02540797910422));
#172991=CARTESIAN_POINT('Ctrl Pts',(20.3653634508192,-17.6027792630595,
5.0249692980654));
#172992=CARTESIAN_POINT('Ctrl Pts',(20.3565758268546,-17.5922290069864,
5.02414968284782));
#172993=CARTESIAN_POINT('Ctrl Pts',(20.3524825493749,-17.5873594966676,
5.02376906056121));
#172994=CARTESIAN_POINT('Ctrl Pts',(20.3433430414357,-17.5765857719689,
5.02292171363795));
#172995=CARTESIAN_POINT('Ctrl Pts',(20.3382861592764,-17.5706907513758,
5.02245455300102));
#172996=CARTESIAN_POINT('Ctrl Pts',(20.3235001590823,-17.553644808404,5.02109335634916));
#172997=CARTESIAN_POINT('Ctrl Pts',(20.3136865635017,-17.5425680785398,
5.02019581449633));
#172998=CARTESIAN_POINT('Ctrl Pts',(20.2348710413583,-17.4554652346242,
5.01303236958278));
#172999=CARTESIAN_POINT('Ctrl Pts',(20.1605477075074,-17.3844584812322,
5.00653638429608));
#173000=CARTESIAN_POINT('Ctrl Pts',(19.9622878213766,-17.2208625695326,
4.98985208558333));
#173001=CARTESIAN_POINT('Ctrl Pts',(19.832814885006,-17.1359245894896,4.9794792746869));
#173002=CARTESIAN_POINT('Ctrl Pts',(19.6471547041593,-17.0413056519028,
4.96600612213582));
#173003=CARTESIAN_POINT('Ctrl Pts',(19.5981223985087,-17.0186355862422,
4.96257237536748));
#173004=CARTESIAN_POINT('Ctrl Pts',(19.540200848538,-16.9945001511946,4.95870136918187));
#173005=CARTESIAN_POINT('Ctrl Pts',(19.5321081526108,-16.9911866868436,
4.95816464068569));
#173006=CARTESIAN_POINT('Ctrl Pts',(19.519830793032,-16.9862484615939,4.95735685104349));
#173007=CARTESIAN_POINT('Ctrl Pts',(19.5156612260621,-16.9845867555206,
4.95708363880995));
#173008=CARTESIAN_POINT('Ctrl Pts',(19.508171175597,-16.9816293001501,4.95659490736115));
#173009=CARTESIAN_POINT('Ctrl Pts',(19.5048526906678,-16.9803286699272,
4.95637909819435));
#173010=CARTESIAN_POINT('Ctrl Pts',(19.4976392279169,-16.9775224573611,
4.95591156531599));
#173011=CARTESIAN_POINT('Ctrl Pts',(19.4937430880841,-16.976020020952,4.95566003115926));
#173012=CARTESIAN_POINT('Ctrl Pts',(19.4827977870243,-16.9718364328974,
4.95495611122427));
#173013=CARTESIAN_POINT('Ctrl Pts',(19.4757386255172,-16.9691813765175,
4.95450526174506));
#173014=CARTESIAN_POINT('Ctrl Pts',(19.4336808862023,-16.9536188689361,
4.95183695137688));
#173015=CARTESIAN_POINT('Ctrl Pts',(19.3983579757969,-16.9415997036103,
4.94966900134766));
#173016=CARTESIAN_POINT('Ctrl Pts',(19.2815937019356,-16.9052829473468,
4.9426836851965));
#173017=CARTESIAN_POINT('Ctrl Pts',(19.1990013073988,-16.8849524392151,
4.93802495004452));
#173018=CARTESIAN_POINT('Ctrl Pts',(18.9399197219225,-16.8374990788314,
4.92368659589947));
#173019=CARTESIAN_POINT('Ctrl Pts',(18.7610973104413,-16.8276703962925,
4.91410957790419));
#173020=CARTESIAN_POINT('Ctrl Pts',(18.5604566308968,-16.8420023720653,
4.90241830992957));
#173021=CARTESIAN_POINT('Ctrl Pts',(18.5377768143958,-16.8439905851481,
4.90108435087472));
#173022=CARTESIAN_POINT('Ctrl Pts',(18.5056759114268,-16.8473272144179,
4.89917694942165));
#173023=CARTESIAN_POINT('Ctrl Pts',(18.4962245754309,-16.8483740192756,
4.89861298266469));
#173024=CARTESIAN_POINT('Ctrl Pts',(18.4808613441585,-16.8501804681498,
4.89769226024643));
#173025=CARTESIAN_POINT('Ctrl Pts',(18.4749449729642,-16.8509014741339,
4.89733672655739));
#173026=CARTESIAN_POINT('Ctrl Pts',(18.4625525391915,-16.8524648313052,
4.89658997074541));
#173027=CARTESIAN_POINT('Ctrl Pts',(18.456077180921,-16.8533121828825,4.89619859423836));
#173028=CARTESIAN_POINT('Ctrl Pts',(18.4406551583803,-16.8554029018133,
4.89526361932241));
#173029=CARTESIAN_POINT('Ctrl Pts',(18.4317123822986,-16.8566735861777,
4.89471916216865));
#173030=CARTESIAN_POINT('Ctrl Pts',(18.4014850482065,-16.8611661431394,
4.8928709386469));
#173031=CARTESIAN_POINT('Ctrl Pts',(18.3802421343791,-16.8646553401602,
4.89155874596095));
#173032=CARTESIAN_POINT('Ctrl Pts',(18.1813146057088,-16.9004534618432,
4.87914154751217));
#173033=CARTESIAN_POINT('Ctrl Pts',(18.0084285223842,-16.9550461715309,
4.86728210648543));
#173034=CARTESIAN_POINT('Ctrl Pts',(17.7363591800773,-17.0810027225583,
4.84747615314401));
#173035=CARTESIAN_POINT('Ctrl Pts',(17.6325274989788,-17.1401824166858,
4.83962887022806));
#173036=CARTESIAN_POINT('Ctrl Pts',(17.5263848639483,-17.2131943061605,
4.83167172260674));
#173037=CARTESIAN_POINT('Ctrl Pts',(17.5185807529136,-17.2186403664178,
4.83108715121268));
#173038=CARTESIAN_POINT('Ctrl Pts',(17.5070715754884,-17.2267879377201,
4.83022607957612));
#173039=CARTESIAN_POINT('Ctrl Pts',(17.503338259817,-17.2294490716168,4.82994692961862));
#173040=CARTESIAN_POINT('Ctrl Pts',(17.4967965708902,-17.2341441567271,
4.82945811851666));
#173041=CARTESIAN_POINT('Ctrl Pts',(17.4939845240037,-17.2361728982267,
4.82924810448511));
#173042=CARTESIAN_POINT('Ctrl Pts',(17.491164892823,-17.2382176635852,4.82903763801035));
#173043=CARTESIAN_POINT('Ctrl Pts',(17.4911523728596,-17.2382267431335,
4.82903670348161));
#173044=CARTESIAN_POINT('Ctrl Pts',(17.4911275513973,-17.2382447442137,
4.82903485073532));
#173045=CARTESIAN_POINT('Ctrl Pts',(17.4911152499266,-17.2382536657177,
4.82903393251981));
#173046=CARTESIAN_POINT('Ctrl Pts',(17.4910908606305,-17.2382713541827,
4.82903211204004));
#173047=CARTESIAN_POINT('Ctrl Pts',(17.4910787727824,-17.2382801211532,
4.82903120977402));
#173048=CARTESIAN_POINT('Ctrl Pts',(17.4910548064742,-17.2382975036179,
4.82902942087523));
#173049=CARTESIAN_POINT('Ctrl Pts',(17.4910429278426,-17.2383061192298,
4.8290285342296));
#173050=CARTESIAN_POINT('Ctrl Pts',(17.4910193741398,-17.2383232031844,
4.82902677613641));
#173051=CARTESIAN_POINT('Ctrl Pts',(17.491007699632,-17.238331671112,4.82902590473084));
#173052=CARTESIAN_POINT('Ctrl Pts',(17.4909845508505,-17.2383484620914,
4.82902417686927));
#173053=CARTESIAN_POINT('Ctrl Pts',(17.4909730763056,-17.2383567853337,
4.82902332039297));
#173054=CARTESIAN_POINT('Ctrl Pts',(17.4909503232398,-17.2383732899781,
4.82902162207552));
#173055=CARTESIAN_POINT('Ctrl Pts',(17.4909390444557,-17.2383814715651,
4.82902078021466));
#173056=CARTESIAN_POINT('Ctrl Pts',(17.4909166782863,-17.2383976962361,
4.82901911078267));
#173057=CARTESIAN_POINT('Ctrl Pts',(17.4909055909967,-17.238405739245,4.82901828321862));
#173058=CARTESIAN_POINT('Ctrl Pts',(17.4908836033598,-17.2384216899757,
4.82901664204743));
#173059=CARTESIAN_POINT('Ctrl Pts',(17.4908727032694,-17.2384295975056,
4.82901582845942));
#173060=CARTESIAN_POINT('Ctrl Pts',(17.4908510867112,-17.2384452796703,
4.82901421499234));
#173061=CARTESIAN_POINT('Ctrl Pts',(17.4908403700331,-17.2384530544523,
4.82901341509752));
#173062=CARTESIAN_POINT('Ctrl Pts',(17.490819116412,-17.2384684739256,4.82901182872651));
#173063=CARTESIAN_POINT('Ctrl Pts',(17.4908085793549,-17.2384761186946,
4.82901104224176));
#173064=CARTESIAN_POINT('Ctrl Pts',(17.4907876807863,-17.2384912811663,
4.82900948237801));
#173065=CARTESIAN_POINT('Ctrl Pts',(17.4907773194862,-17.2384987987107,
4.82900870901474));
#173066=CARTESIAN_POINT('Ctrl Pts',(17.4907572863614,-17.2385133338344,
4.82900721375325));
#173067=CARTESIAN_POINT('Ctrl Pts',(17.4907476147675,-17.2385203512278,
4.82900649187207));
#173068=CARTESIAN_POINT('Ctrl Pts',(17.4907283082907,-17.2385343596279,
4.82900505085238));
#173069=CARTESIAN_POINT('Ctrl Pts',(17.4907186731607,-17.2385413508128,
4.82900433169542));
#173070=CARTESIAN_POINT('Ctrl Pts',(17.4906994389801,-17.2385553072514,
4.82900289607701));
#173071=CARTESIAN_POINT('Ctrl Pts',(17.4906898399113,-17.2385622725173,
4.82900217961419));
#173072=CARTESIAN_POINT('Ctrl Pts',(17.4906706776621,-17.2385761772538,
4.82900074936975));
#173073=CARTESIAN_POINT('Ctrl Pts',(17.4906611144548,-17.2385831167428,
4.82900003558613));
#173074=CARTESIAN_POINT('Ctrl Pts',(17.4873595633594,-17.2409789114267,
4.82875361314171));
#173075=CARTESIAN_POINT('Ctrl Pts',(17.4840744353518,-17.2433772718097,
4.82850856674509));
#173076=CARTESIAN_POINT('Ctrl Pts',(17.4772837403103,-17.2483649933542,
4.82800229636659));
#173077=CARTESIAN_POINT('Ctrl Pts',(17.4737792121438,-17.2509557442992,
4.82774116884939));
#173078=CARTESIAN_POINT('Ctrl Pts',(17.4648886357129,-17.25757073086,4.82707902482906));
#173079=CARTESIAN_POINT('Ctrl Pts',(17.4595136673081,-17.2616098694312,
4.82667899986179));
#173080=CARTESIAN_POINT('Ctrl Pts',(17.4440675041607,-17.2733327843016,
4.82552997832671));
#173081=CARTESIAN_POINT('Ctrl Pts',(17.4340457362834,-17.2810815718692,
4.82478513649517));
#173082=CARTESIAN_POINT('Ctrl Pts',(17.3998992444123,-17.307976670175,4.82224727187036));
#173083=CARTESIAN_POINT('Ctrl Pts',(17.3761221193629,-17.3275599775156,
4.82048004543612));
#173084=CARTESIAN_POINT('Ctrl Pts',(17.2576046163725,-17.4295947020338,
4.81162244029538));
#173085=CARTESIAN_POINT('Ctrl Pts',(17.1699023948968,-17.5198460840967,
4.80489273819077));
#173086=CARTESIAN_POINT('Ctrl Pts',(17.0703323498763,-17.6424412566836,
4.79629573249236));
#173087=CARTESIAN_POINT('Ctrl Pts',(17.0505285847102,-17.6679991863497,
4.79453089435811));
#173088=CARTESIAN_POINT('Ctrl Pts',(16.9677514087738,-17.7800367236019,
4.78687724020415));
#173089=CARTESIAN_POINT('Ctrl Pts',(16.9108049776667,-17.8707564587531,
4.78087640088961));
#173090=CARTESIAN_POINT('Ctrl Pts',(16.8543804800283,-17.9778753612386,
4.77378206341766));
#173091=CARTESIAN_POINT('Ctrl Pts',(16.8479255629668,-17.9904327609149,
4.77295047080033));
#173092=CARTESIAN_POINT('Ctrl Pts',(16.8378292523889,-18.0105669742307,
4.77161679850807));
#173093=CARTESIAN_POINT('Ctrl Pts',(16.8341064723427,-18.0181026680824,
4.7711175714359));
#173094=CARTESIAN_POINT('Ctrl Pts',(16.8276068936708,-18.0314589030616,
4.77023253496533));
#173095=CARTESIAN_POINT('Ctrl Pts',(16.8248116151471,-18.0372703695984,
4.76984737533886));
#173096=CARTESIAN_POINT('Ctrl Pts',(16.819072493442,-18.0493430809861,4.76904706285574));
#173097=CARTESIAN_POINT('Ctrl Pts',(16.8161327079192,-18.0556061596514,
4.76863177503638));
#173098=CARTESIAN_POINT('Ctrl Pts',(16.8086396505514,-18.0717753764283,
4.76755931972236));
#173099=CARTESIAN_POINT('Ctrl Pts',(16.8041321485649,-18.0817023887174,
4.7669005840777));
#173100=CARTESIAN_POINT('Ctrl Pts',(16.7854245684037,-18.1237627314918,
4.76410794969152));
#173101=CARTESIAN_POINT('Ctrl Pts',(16.7719494902557,-18.1562106116635,
4.76194949610491));
#173102=CARTESIAN_POINT('Ctrl Pts',(16.7545505706728,-18.2012392122745,
4.75894686365453));
#173103=CARTESIAN_POINT('Ctrl Pts',(16.7499273310879,-18.2135439171612,
4.75812563213439));
#173104=CARTESIAN_POINT('Ctrl Pts',(16.7454193672347,-18.225889769394,4.75730093103984));
#173105=CARTESIAN_POINT('Ctrl Pts',(16.7454193964829,-18.2258896892926,
4.53222340662745));
#173106=CARTESIAN_POINT('Ctrl Pts',(16.754772318456,-18.200275069933,4.53397284136854));
#173107=CARTESIAN_POINT('Ctrl Pts',(16.7646214421699,-18.1748376104556,
4.53573525615426));
#173108=CARTESIAN_POINT('Ctrl Pts',(16.8069131799647,-18.0715845407491,
4.54298738003099));
#173109=CARTESIAN_POINT('Ctrl Pts',(16.8434938433157,-17.9955585372352,
4.54856233763303));
#173110=CARTESIAN_POINT('Ctrl Pts',(16.9297103717033,-17.8407581583082,
4.5602682192208));
#173111=CARTESIAN_POINT('Ctrl Pts',(16.9802103467348,-17.7626540023637,
4.56638569977088));
#173112=CARTESIAN_POINT('Ctrl Pts',(17.0541238084425,-17.6633343328212,
4.5742404025468));
#173113=CARTESIAN_POINT('Ctrl Pts',(17.0731072755806,-17.6389581837111,
4.57617427513876));
#173114=CARTESIAN_POINT('Ctrl Pts',(17.0971189102555,-17.6094799534252,
4.57851166140639));
#173115=CARTESIAN_POINT('Ctrl Pts',(17.1016471801378,-17.6039777256158,
4.57894788660996));
#173116=CARTESIAN_POINT('Ctrl Pts',(17.1088147078132,-17.5953576558042,
4.5796310650876));
#173117=CARTESIAN_POINT('Ctrl Pts',(17.111435305927,-17.5922244677135,4.57987933492333));
#173118=CARTESIAN_POINT('Ctrl Pts',(17.1163670238579,-17.5863626613758,
4.58034369213323));
#173119=CARTESIAN_POINT('Ctrl Pts',(17.1186759616822,-17.5836323456073,
4.58055992558959));
#173120=CARTESIAN_POINT('Ctrl Pts',(17.1239841426583,-17.5773875873574,
4.58105438511289));
#173121=CARTESIAN_POINT('Ctrl Pts',(17.1269879753649,-17.5738771101644,
4.58133226895676));
#173122=CARTESIAN_POINT('Ctrl Pts',(17.1348968945598,-17.5646952456248,
4.58205897836552));
#173123=CARTESIAN_POINT('Ctrl Pts',(17.1398207111901,-17.5590399782331,
4.58250645781604));
#173124=CARTESIAN_POINT('Ctrl Pts',(17.1732971584306,-17.5210004842219,
4.58551655451351));
#173125=CARTESIAN_POINT('Ctrl Pts',(17.2028067799057,-17.4894676521047,
4.5880127018827));
#173126=CARTESIAN_POINT('Ctrl Pts',(17.2841891408324,-17.4076713448506,
4.59456112287321));
#173127=CARTESIAN_POINT('Ctrl Pts',(17.3377047382897,-17.3591210282201,
4.59852801774289));
#173128=CARTESIAN_POINT('Ctrl Pts',(17.4624292677644,-17.2570945701982,
4.60731084102632));
#173129=CARTESIAN_POINT('Ctrl Pts',(17.5347367473087,-17.2051846040635,
4.61210402565903));
#173130=CARTESIAN_POINT('Ctrl Pts',(17.6710014414909,-17.1198185781199,
4.62094191479838));
#173131=CARTESIAN_POINT('Ctrl Pts',(17.7338083413045,-17.0847908206052,
4.62494721111515));
#173132=CARTESIAN_POINT('Ctrl Pts',(17.8227977656424,-17.0409408466135,
4.63062111952317));
#173133=CARTESIAN_POINT('Ctrl Pts',(17.8475550973671,-17.0293320778753,
4.6321992403569));
#173134=CARTESIAN_POINT('Ctrl Pts',(17.8907948774613,-17.0100695295552,
4.63495923152697));
#173135=CARTESIAN_POINT('Ctrl Pts',(17.9091740820108,-17.0021920619488,
4.63613350538952));
#173136=CARTESIAN_POINT('Ctrl Pts',(17.9357442339642,-16.99124679124,4.63783385888435));
#173137=CARTESIAN_POINT('Ctrl Pts',(17.9438472553281,-16.9879674009152,
4.63835277178358));
#173138=CARTESIAN_POINT('Ctrl Pts',(17.9580199490438,-16.9823334437839,
4.63926110786267));
#173139=CARTESIAN_POINT('Ctrl Pts',(17.9640806427731,-16.9799565004632,
4.63964977092109));
#173140=CARTESIAN_POINT('Ctrl Pts',(17.9757332274125,-16.9754483785895,
4.64039751280649));
#173141=CARTESIAN_POINT('Ctrl Pts',(17.9813233875882,-16.9733128780688,
4.64075644189779));
#173142=CARTESIAN_POINT('Ctrl Pts',(17.9959434004303,-16.9677987983539,
4.64169574023316));
#173143=CARTESIAN_POINT('Ctrl Pts',(18.0049873357343,-16.9644581807389,
4.64227737278311));
#173144=CARTESIAN_POINT('Ctrl Pts',(18.0362140946776,-16.9531655549944,
4.64428780762626));
#173145=CARTESIAN_POINT('Ctrl Pts',(18.0585060534235,-16.9455224481869,
4.64572680546249));
#173146=CARTESIAN_POINT('Ctrl Pts',(18.2397818338403,-16.8867327617592,
4.65746335188572));
#173147=CARTESIAN_POINT('Ctrl Pts',(18.4041534451225,-16.8542008464835,
4.66839028012184));
#173148=CARTESIAN_POINT('Ctrl Pts',(18.6959290106786,-16.8316130817408,
4.68772987662371));
#173149=CARTESIAN_POINT('Ctrl Pts',(18.8218850191862,-16.8330915692602,
4.69603740526457));
#173150=CARTESIAN_POINT('Ctrl Pts',(18.9588884424978,-16.8469447636106,
4.70457748661341));
#173151=CARTESIAN_POINT('Ctrl Pts',(18.9707908796195,-16.8482503822106,
4.70531515341339));
#173152=CARTESIAN_POINT('Ctrl Pts',(18.9876807360557,-16.8502482491841,
4.70635523972687));
#173153=CARTESIAN_POINT('Ctrl Pts',(18.9926774971707,-16.8508573842878,
4.70666211073343));
#173154=CARTESIAN_POINT('Ctrl Pts',(19.0012791776244,-16.851937130166,4.70718888456338));
#173155=CARTESIAN_POINT('Ctrl Pts',(19.0048851290856,-16.8523992132633,
4.70740926396949));
#173156=CARTESIAN_POINT('Ctrl Pts',(19.0118699263502,-16.8533125712208,
4.70783524715647));
#173157=CARTESIAN_POINT('Ctrl Pts',(19.0152488725661,-16.8537627179592,
4.70804091578542));
#173158=CARTESIAN_POINT('Ctrl Pts',(19.0243527712292,-16.8549979353352,
4.70859399576695));
#173159=CARTESIAN_POINT('Ctrl Pts',(19.0300756695645,-16.8557982943802,
4.70894054992581));
#173160=CARTESIAN_POINT('Ctrl Pts',(19.0512482991217,-16.8588477681515,
4.71021875029902));
#173161=CARTESIAN_POINT('Ctrl Pts',(19.0666767188995,-16.8612443993234,
4.71114243008841));
#173162=CARTESIAN_POINT('Ctrl Pts',(19.2162964974428,-16.8861843472443,
4.7200369313936));
#173163=CARTESIAN_POINT('Ctrl Pts',(19.3480651140697,-16.9214487168096,
4.72738951779247));
#173164=CARTESIAN_POINT('Ctrl Pts',(19.6208322890261,-17.0234574446481,
4.74320404432964));
#173165=CARTESIAN_POINT('Ctrl Pts',(19.7596839715869,-17.093583251869,4.75165261966882));
#173166=CARTESIAN_POINT('Ctrl Pts',(19.9074470798247,-17.1898526076665,
4.76192312841269));
#173167=CARTESIAN_POINT('Ctrl Pts',(19.9250932814396,-17.2017319554377,
4.7631713912118));
#173168=CARTESIAN_POINT('Ctrl Pts',(19.9499376985908,-17.2190068308189,
4.76496143502447));
#173169=CARTESIAN_POINT('Ctrl Pts',(19.957285523834,-17.2241856770287,4.765494978814));
#173170=CARTESIAN_POINT('Ctrl Pts',(19.9699075633757,-17.2332027342146,
4.76641876189396));
#173171=CARTESIAN_POINT('Ctrl Pts',(19.9751974716944,-17.2370188394995,
4.76680814699667));
#173172=CARTESIAN_POINT('Ctrl Pts',(19.9852943241552,-17.2443738277718,
4.76755568472128));
#173173=CARTESIAN_POINT('Ctrl Pts',(19.9901041092418,-17.247908718597,4.76791367995835));
#173174=CARTESIAN_POINT('Ctrl Pts',(20.0025768327709,-17.2571568859452,
4.76884701316293));
#173175=CARTESIAN_POINT('Ctrl Pts',(20.010216078317,-17.2629017557701,4.76942358320949));
#173176=CARTESIAN_POINT('Ctrl Pts',(20.0361560695647,-17.2826855967837,
4.77139846845714));
#173177=CARTESIAN_POINT('Ctrl Pts',(20.0542656587715,-17.2969714411774,
4.77280650147324));
#173178=CARTESIAN_POINT('Ctrl Pts',(20.207352452308,-17.4218464405586,4.78496745277203));
#173179=CARTESIAN_POINT('Ctrl Pts',(20.3283874709806,-17.5484178328147,
4.79641507488717));
#173180=CARTESIAN_POINT('Ctrl Pts',(20.4848581117967,-17.7587363930967,
4.81373567188046));
#173181=CARTESIAN_POINT('Ctrl Pts',(20.532791902547,-17.8322983480734,4.81951805212073));
#173182=CARTESIAN_POINT('Ctrl Pts',(20.5947541019857,-17.9416895947832,
4.82754598929554));
#173183=CARTESIAN_POINT('Ctrl Pts',(20.6125899992041,-17.9752538849689,
4.82993652355876));
#173184=CARTESIAN_POINT('Ctrl Pts',(20.6328900403606,-18.0160709973614,
4.83274178051278));
#173185=CARTESIAN_POINT('Ctrl Pts',(20.6362298347509,-18.0228777566229,
4.8332062556453));
#173186=CARTESIAN_POINT('Ctrl Pts',(20.6413560446168,-18.0334688745061,
4.83392363046653));
#173187=CARTESIAN_POINT('Ctrl Pts',(20.6431678902856,-18.0372407547124,
4.83417806927643));
#173188=CARTESIAN_POINT('Ctrl Pts',(20.6465020140673,-18.044234752239,4.83464789617231));
#173189=CARTESIAN_POINT('Ctrl Pts',(20.6480273271511,-18.0474553133902,
4.83486346719623));
#173190=CARTESIAN_POINT('Ctrl Pts',(20.6514506883045,-18.054730863922,4.83534873327727));
#173191=CARTESIAN_POINT('Ctrl Pts',(20.6533440037885,-18.0587880203415,
4.83561813427794));
#173192=CARTESIAN_POINT('Ctrl Pts',(20.6588751268934,-18.0707393707925,
4.83640827253624));
#173193=CARTESIAN_POINT('Ctrl Pts',(20.6624772549224,-18.0786501080127,
4.83692686193532));
#173194=CARTESIAN_POINT('Ctrl Pts',(20.6875902756344,-18.1347145519584,
4.84057262004026));
#173195=CARTESIAN_POINT('Ctrl Pts',(20.7073457422561,-18.1836393823493,
4.84360071800973));
#173196=CARTESIAN_POINT('Ctrl Pts',(20.7306225801284,-18.2481269597652,
4.84745835617574));
#173197=CARTESIAN_POINT('Ctrl Pts',(20.735823873816,-18.2630586525973,4.84834244346051));
#173198=CARTESIAN_POINT('Ctrl Pts',(20.7570349475525,-18.3262197808785,
4.85204911562008));
#173199=CARTESIAN_POINT('Ctrl Pts',(20.7714732402945,-18.374960639018,4.8548291864931));
#173200=CARTESIAN_POINT('Ctrl Pts',(20.811422380871,-18.5301286100413,4.86355297288325));
#173201=CARTESIAN_POINT('Ctrl Pts',(20.8304458149371,-18.6380361702916,
4.86944393682973));
#173202=CARTESIAN_POINT('Ctrl Pts',(20.846389206078,-18.8018475032445,4.87859495474299));
#173203=CARTESIAN_POINT('Ctrl Pts',(20.8495848950305,-18.8569535131039,
4.88170630147725));
#173204=CARTESIAN_POINT('Ctrl Pts',(20.8512712239753,-18.9464523135157,
4.8868560873045));
#173205=CARTESIAN_POINT('Ctrl Pts',(20.8510826304748,-18.9807949876418,
4.88885502266212));
#173206=CARTESIAN_POINT('Ctrl Pts',(20.8497365406336,-19.0259243042199,
4.89151775477155));
#173207=CARTESIAN_POINT('Ctrl Pts',(20.8493313807709,-19.0367293047743,
4.89215797610226));
#173208=CARTESIAN_POINT('Ctrl Pts',(20.8485321517945,-19.0544225315507,
4.89321094644742));
#173209=CARTESIAN_POINT('Ctrl Pts',(20.8481871471625,-19.0613128582669,
4.89362215266174));
#173210=CARTESIAN_POINT('Ctrl Pts',(20.84745407647,-19.0746480865406,4.8944202480048));
#173211=CARTESIAN_POINT('Ctrl Pts',(20.8470701938352,-19.0810931484332,
4.8948070014158));
#173212=CARTESIAN_POINT('Ctrl Pts',(20.846115669035,-19.0959716965935,4.89570223994669));
#173213=CARTESIAN_POINT('Ctrl Pts',(20.8455239908086,-19.1044036804215,
4.89621138054998));
#173214=CARTESIAN_POINT('Ctrl Pts',(20.8437967267627,-19.1270736393192,
4.89758515543206));
#173215=CARTESIAN_POINT('Ctrl Pts',(20.8425675337751,-19.1413038490304,
4.89845271424219));
#173216=CARTESIAN_POINT('Ctrl Pts',(20.8276339788592,-19.2959218893946,
4.90793753224795));
#173217=CARTESIAN_POINT('Ctrl Pts',(20.8000780806493,-19.4345904264661,
4.91700446926346));
#173218=CARTESIAN_POINT('Ctrl Pts',(20.7307657611253,-19.6618965447862,
4.9326383499417));
#173219=CARTESIAN_POINT('Ctrl Pts',(20.6962859582462,-19.7522878394038,
4.93906620081814));
#173220=CARTESIAN_POINT('Ctrl Pts',(20.6352154251679,-19.8844515525025,
4.94856682673797));
#173221=CARTESIAN_POINT('Ctrl Pts',(20.6131418038496,-19.9281724769969,
4.9517262946967));
#173222=CARTESIAN_POINT('Ctrl Pts',(20.5769349017628,-19.9940983322026,
4.95647585431921));
#173223=CARTESIAN_POINT('Ctrl Pts',(20.5638717655726,-20.0168696888842,
4.95811355220475));
#173224=CARTESIAN_POINT('Ctrl Pts',(20.5469161354676,-20.0451924660992,
4.96014129875251));
#173225=CARTESIAN_POINT('Ctrl Pts',(20.5434166529492,-20.0509750047458,
4.96055480325799));
#173226=CARTESIAN_POINT('Ctrl Pts',(20.5378004231564,-20.0601557017502,
4.96121039766653));
#173227=CARTESIAN_POINT('Ctrl Pts',(20.5357016616382,-20.0635647299935,
4.96145363570265));
#173228=CARTESIAN_POINT('Ctrl Pts',(20.5317008673729,-20.070022138123,4.96191396606396));
#173229=CARTESIAN_POINT('Ctrl Pts',(20.5298007682063,-20.0730715904659,
4.96213117331686));
#173230=CARTESIAN_POINT('Ctrl Pts',(20.5254067434013,-20.0800836853035,
4.96263024271057));
#173231=CARTESIAN_POINT('Ctrl Pts',(20.5229074300434,-20.0840429007112,
4.96291174500148));
#173232=CARTESIAN_POINT('Ctrl Pts',(20.5161685919782,-20.0946399885494,
4.96366452749176));
#173233=CARTESIAN_POINT('Ctrl Pts',(20.5119050780741,-20.1012626207208,
4.96413426295707));
#173234=CARTESIAN_POINT('Ctrl Pts',(20.4795573094514,-20.1508984604032,
4.96765070155067));
#173235=CARTESIAN_POINT('Ctrl Pts',(20.4499503115872,-20.1929042217322,
4.97060301945223));
#173236=CARTESIAN_POINT('Ctrl Pts',(20.405322651057,-20.2515645953815,4.97475506271402));
#173237=CARTESIAN_POINT('Ctrl Pts',(20.3915229145882,-20.2691201075979,
4.97600158804748));
#173238=CARTESIAN_POINT('Ctrl Pts',(20.34849985572,-20.3221051671264,4.97978668947714));
#173239=CARTESIAN_POINT('Ctrl Pts',(20.31839877085,-20.3568055840512,4.98229787485677));
#173240=CARTESIAN_POINT('Ctrl Pts',(20.2128871884547,-20.4707296129182,
4.99075189091243));
#173241=CARTESIAN_POINT('Ctrl Pts',(20.1324783320613,-20.54508016895,4.99664011080124));
#173242=CARTESIAN_POINT('Ctrl Pts',(20.0034506055505,-20.6470580023039,
5.00578474865274));
#173243=CARTESIAN_POINT('Ctrl Pts',(19.9588963512765,-20.6795285104071,
5.00889243798102));
#173244=CARTESIAN_POINT('Ctrl Pts',(19.8846336888657,-20.729331771879,5.01403670977699));
#173245=CARTESIAN_POINT('Ctrl Pts',(19.8556800796864,-20.7477448915421,
5.01603389934779));
#173246=CARTESIAN_POINT('Ctrl Pts',(19.8170338156994,-20.7710227019625,
5.01869463528502));
#173247=CARTESIAN_POINT('Ctrl Pts',(19.8077321939334,-20.7765287077368,
5.01933465131812));
#173248=CARTESIAN_POINT('Ctrl Pts',(19.7924260374679,-20.7854314572724,
5.02038736999084));
#173249=CARTESIAN_POINT('Ctrl Pts',(19.7864462707031,-20.7888705536475,
5.02079853127742));
#173250=CARTESIAN_POINT('Ctrl Pts',(19.7748370293323,-20.7954719875448,
5.02159660086907));
#173251=CARTESIAN_POINT('Ctrl Pts',(19.769209679183,-20.7986379204339,5.0219833737817));
#173252=CARTESIAN_POINT('Ctrl Pts',(19.7561805473098,-20.8058898051277,
5.02287874696172));
#173253=CARTESIAN_POINT('Ctrl Pts',(19.7487686329828,-20.8099572382404,
5.02338800333369));
#173254=CARTESIAN_POINT('Ctrl Pts',(19.7287643514983,-20.8207795694781,
5.02476229315683));
#173255=CARTESIAN_POINT('Ctrl Pts',(19.7161277950838,-20.8274514583743,
5.02563025455207));
#173256=CARTESIAN_POINT('Ctrl Pts',(19.5995666347805,-20.8874926935597,
5.03363619915195));
#173257=CARTESIAN_POINT('Ctrl Pts',(19.4914754346517,-20.9322930917346,
5.04107584411056));
#173258=CARTESIAN_POINT('Ctrl Pts',(19.2253670958755,-21.0176000717807,
5.05932905993716));
#173259=CARTESIAN_POINT('Ctrl Pts',(19.0652754111759,-21.0492367399968,
5.07028251195642));
#173260=CARTESIAN_POINT('Ctrl Pts',(18.8706544515756,-21.0648361836614,
5.08268978694441));
#173261=CARTESIAN_POINT('Ctrl Pts',(18.8381096402168,-21.0666897246284,
5.08473256954471));
#173262=CARTESIAN_POINT('Ctrl Pts',(18.7982918666113,-21.0680359283952,
5.08718250355468));
#173263=CARTESIAN_POINT('Ctrl Pts',(18.7910493736998,-21.0682435745509,
5.08762612892618));
#173264=CARTESIAN_POINT('Ctrl Pts',(18.7796960555114,-21.068510753617,5.08831827726249));
#173265=CARTESIAN_POINT('Ctrl Pts',(18.7755859595699,-21.0685954994511,
5.08856817367552));
#173266=CARTESIAN_POINT('Ctrl Pts',(18.7679044559218,-21.0687315004401,
5.08903392288986));
#173267=CARTESIAN_POINT('Ctrl Pts',(18.7643332045736,-21.0687856892039,
5.08924993161544));
#173268=CARTESIAN_POINT('Ctrl Pts',(18.7561826605718,-21.0688887313678,
5.08974173868459));
#173269=CARTESIAN_POINT('Ctrl Pts',(18.7516033448229,-21.0689317642705,
5.09001720848254));
#173270=CARTESIAN_POINT('Ctrl Pts',(18.737534159529,-21.0690183201493,5.09086103663999));
#173271=CARTESIAN_POINT('Ctrl Pts',(18.7280439575885,-21.0690128935072,
5.09142672702305));
#173272=CARTESIAN_POINT('Ctrl Pts',(18.6431563082706,-21.0683935185377,
5.09645789482124));
#173273=CARTESIAN_POINT('Ctrl Pts',(18.5678330642437,-21.0638156197783,
5.10071966128931));
#173274=CARTESIAN_POINT('Ctrl Pts',(18.450068703757,-21.0503162925105,5.10728216443256));
#173275=CARTESIAN_POINT('Ctrl Pts',(18.4073891580195,-21.0440979409608,
5.10963935816056));
#173276=CARTESIAN_POINT('Ctrl Pts',(18.2572776141251,-21.0175209278849,
5.11793903805176));
#173277=CARTESIAN_POINT('Ctrl Pts',(18.1512660832122,-20.9901514252831,
5.12382591142329));
#173278=CARTESIAN_POINT('Ctrl Pts',(17.9957399364974,-20.9368664675411,
5.13296741886644));
#173279=CARTESIAN_POINT('Ctrl Pts',(17.9443529688159,-20.9169884826622,
5.13607331392347));
#173280=CARTESIAN_POINT('Ctrl Pts',(17.8623244915629,-20.8815198603959,
5.14121488036626));
#173281=CARTESIAN_POINT('Ctrl Pts',(17.8311837891009,-20.8671469334335,
5.14321121316726));
#173282=CARTESIAN_POINT('Ctrl Pts',(17.7907074600633,-20.8472585530818,
5.1458709694105));
#173283=CARTESIAN_POINT('Ctrl Pts',(17.7810445492673,-20.8424183931852,
5.14651088463052));
#173284=CARTESIAN_POINT('Ctrl Pts',(17.7652757072066,-20.8343681426957,
5.14756347971931));
#173285=CARTESIAN_POINT('Ctrl Pts',(17.7591475806824,-20.8312017823808,
5.14797461894549));
#173286=CARTESIAN_POINT('Ctrl Pts',(17.7473131699517,-20.8250135589137,
5.14877267590951));
#173287=CARTESIAN_POINT('Ctrl Pts',(17.7416050148993,-20.8219954236787,
5.14915945841463));
#173288=CARTESIAN_POINT('Ctrl Pts',(17.7284539648584,-20.8149647521691,
5.15005489779027));
#173289=CARTESIAN_POINT('Ctrl Pts',(17.7210211612614,-20.8109336635934,
5.15056421107067));
#173290=CARTESIAN_POINT('Ctrl Pts',(17.7010897608731,-20.7999690809423,
5.15193875404837));
#173291=CARTESIAN_POINT('Ctrl Pts',(17.6886370695332,-20.7929534524509,
5.15280691336821));
#173292=CARTESIAN_POINT('Ctrl Pts',(17.5748446652883,-20.7273179688134,
5.16082807579894));
#173293=CARTESIAN_POINT('Ctrl Pts',(17.4784763014697,-20.6605219849814,
5.16828407250825));
#173294=CARTESIAN_POINT('Ctrl Pts',(17.2619802702192,-20.4822146764628,
5.1866057889009));
#173295=CARTESIAN_POINT('Ctrl Pts',(17.1482855190796,-20.3640583589844,
5.19761341248368));
#173296=CARTESIAN_POINT('Ctrl Pts',(17.0301312372366,-20.20879106028,5.21000148021404));
#173297=CARTESIAN_POINT('Ctrl Pts',(17.0115145700478,-20.1831525995034,
5.21198579601905));
#173298=CARTESIAN_POINT('Ctrl Pts',(16.9893908703803,-20.151199552754,5.21437539162412));
#173299=CARTESIAN_POINT('Ctrl Pts',(16.9853324635605,-20.1452738298009,
5.21481510182035));
#173300=CARTESIAN_POINT('Ctrl Pts',(16.9790064012734,-20.1359354939914,
5.21550250549595));
#173301=CARTESIAN_POINT('Ctrl Pts',(16.97671840577,-20.1325368205786,5.21575154220205));
#173302=CARTESIAN_POINT('Ctrl Pts',(16.9724531169237,-20.1261611263267,
5.21621655077545));
#173303=CARTESIAN_POINT('Ctrl Pts',(16.9704735177931,-20.1231857746006,
5.21643267337742));
#173304=CARTESIAN_POINT('Ctrl Pts',(16.9659626667949,-20.1163685647674,
5.21692585995881));
#173305=CARTESIAN_POINT('Ctrl Pts',(16.963436402639,-20.1125234658731,5.21720258826067));
#173306=CARTESIAN_POINT('Ctrl Pts',(16.9568612413429,-20.1024443004704,
5.21792429528379));
#173307=CARTESIAN_POINT('Ctrl Pts',(16.9528325684129,-20.0961970286344,
5.21836795778722));
#173308=CARTESIAN_POINT('Ctrl Pts',(16.9263026459696,-20.0545773327195,
5.22130031036703));
#173309=CARTESIAN_POINT('Ctrl Pts',(16.9048218062812,-20.0185618413852,
5.22372636744759));
#173310=CARTESIAN_POINT('Ctrl Pts',(16.8738470304827,-19.9629364588946,
5.22734407529229));
#173311=CARTESIAN_POINT('Ctrl Pts',(16.8635636945988,-19.9437810610351,
5.22856737227146));
#173312=CARTESIAN_POINT('Ctrl Pts',(16.8457316295034,-19.9092999763928,
5.23073541025197));
#173313=CARTESIAN_POINT('Ctrl Pts',(16.8380700257995,-19.8940351563942,
5.23168355136719));
#173314=CARTESIAN_POINT('Ctrl Pts',(16.7722507223706,-19.7588417841076,
5.23999251737901));
#173315=CARTESIAN_POINT('Ctrl Pts',(16.725354489134,-19.6337616411367,5.24709266585253));
#173316=CARTESIAN_POINT('Ctrl Pts',(16.6648838059536,-19.4103478525176,
5.25986483766746));
#173317=CARTESIAN_POINT('Ctrl Pts',(16.6458617350985,-19.3139386783995,
5.26540003836287));
#173318=CARTESIAN_POINT('Ctrl Pts',(16.6317631833846,-19.20200921222,5.27201864577449));
#173319=CARTESIAN_POINT('Ctrl Pts',(16.6300811152558,-19.1874348095121,
5.27288398235805));
#173320=CARTESIAN_POINT('Ctrl Pts',(16.6277432511404,-19.1651464696357,
5.27421314451305));
#173321=CARTESIAN_POINT('Ctrl Pts',(16.6269780363118,-19.1574442789052,
5.27467352219713));
#173322=CARTESIAN_POINT('Ctrl Pts',(16.6257184970612,-19.144018505712,5.27547791919846));
#173323=CARTESIAN_POINT('Ctrl Pts',(16.625205197021,-19.1382967527706,5.27582133732469));
#173324=CARTESIAN_POINT('Ctrl Pts',(16.624103385343,-19.125426421594,5.27659519695625));
#173325=CARTESIAN_POINT('Ctrl Pts',(16.6235279050008,-19.1182768249215,
5.27702604414088));
#173326=CARTESIAN_POINT('Ctrl Pts',(16.6220830311269,-19.0991085335299,
5.27818379609974));
#173327=CARTESIAN_POINT('Ctrl Pts',(16.6212799116607,-19.0870852433443,
5.27891277238418));
#173328=CARTESIAN_POINT('Ctrl Pts',(16.6181723376117,-19.0337143086554,
5.28216140712792));
#173329=CARTESIAN_POINT('Ctrl Pts',(16.6169788915316,-18.9923134308124,
5.28471557896899));
#173330=CARTESIAN_POINT('Ctrl Pts',(16.617087834612,-18.7814276676958,5.29790820125772));
#173331=CARTESIAN_POINT('Ctrl Pts',(16.6375272207331,-18.6125948183922,
5.30913937462206));
#173332=CARTESIAN_POINT('Ctrl Pts',(16.6963015742312,-18.3727973722924,
5.32541879940326));
#173333=CARTESIAN_POINT('Ctrl Pts',(16.7188568526094,-18.2986358842749,
5.3304889857474));
#173334=CARTESIAN_POINT('Ctrl Pts',(16.7454193844609,-18.2258897222169,
5.33540091855303));
#173335=CARTESIAN_POINT('Origin',(18.734,-18.952,0.));
#173336=CARTESIAN_POINT('',(16.7454193692319,-18.2258897639242,6.35350369657411));
#173337=CARTESIAN_POINT('',(16.7454193692319,-18.2258897639242,6.13370787796071));
#173338=CARTESIAN_POINT('',(16.7454193692319,-18.2258897639242,0.));
#173339=CARTESIAN_POINT('',(16.6170008387226,-18.9506676920045,6.31236769265572));
#173340=CARTESIAN_POINT('Ctrl Pts',(16.7454193692319,-18.2258897639243,
6.3535036965741));
#173341=CARTESIAN_POINT('Ctrl Pts',(16.7445879657081,-18.2281667087484,
6.35335894716062));
#173342=CARTESIAN_POINT('Ctrl Pts',(16.7437604676845,-18.2304450957259,
6.35321441845044));
#173343=CARTESIAN_POINT('Ctrl Pts',(16.7316385710274,-18.2640003541916,
6.35109037726281));
#173344=CARTESIAN_POINT('Ctrl Pts',(16.7210780199771,-18.2955396540834,
6.34915175896324));
#173345=CARTESIAN_POINT('Ctrl Pts',(16.6634370111024,-18.4821822421839,
6.33794484181155));
#173346=CARTESIAN_POINT('Ctrl Pts',(16.6335480199623,-18.6420437528863,
6.32937665650607));
#173347=CARTESIAN_POINT('Ctrl Pts',(16.618764144361,-18.8526586204593,6.31781740961247));
#173348=CARTESIAN_POINT('Ctrl Pts',(16.6170313257821,-18.9016549965022,
6.31511280070357));
#173349=CARTESIAN_POINT('Ctrl Pts',(16.6170004208958,-18.9506650571224,
6.3123685677428));
#173350=CARTESIAN_POINT('Ctrl Pts',(16.6170004192105,-18.950667732362,6.31236841794738));
#173351=CARTESIAN_POINT('Ctrl Pts',(16.6169589235782,-19.0166051114148,
6.30867636740193));
#173352=CARTESIAN_POINT('Ctrl Pts',(16.6199979904649,-19.0825044489203,
6.30491530142379));
#173353=CARTESIAN_POINT('Ctrl Pts',(16.6271997938263,-19.1598966693579,
6.30036722445836));
#173354=CARTESIAN_POINT('Ctrl Pts',(16.6283908363858,-19.1716319094263,
6.29967406401305));
#173355=CARTESIAN_POINT('Ctrl Pts',(16.6305234250977,-19.1910290350328,
6.29852224835313));
#173356=CARTESIAN_POINT('Ctrl Pts',(16.6314089287677,-19.1986969102738,
6.29806534581304));
#173357=CARTESIAN_POINT('Ctrl Pts',(16.6330729561629,-19.212446045737,6.29724317617807));
#173358=CARTESIAN_POINT('Ctrl Pts',(16.6338360029738,-19.2185291178272,
6.29687839895436));
#173359=CARTESIAN_POINT('Ctrl Pts',(16.6354355559125,-19.2308473608446,
6.29613761458187));
#173360=CARTESIAN_POINT('Ctrl Pts',(16.6362734530907,-19.2370822858573,
6.29576156702282));
#173361=CARTESIAN_POINT('Ctrl Pts',(16.6381348447124,-19.2504805029742,
6.29495108088364));
#173362=CARTESIAN_POINT('Ctrl Pts',(16.6391672979084,-19.2576424512848,
6.2945163629894));
#173363=CARTESIAN_POINT('Ctrl Pts',(16.642059177247,-19.2769996537484,6.29333735088658));
#173364=CARTESIAN_POINT('Ctrl Pts',(16.6439884938243,-19.2891840369773,
6.2925908510825));
#173365=CARTESIAN_POINT('Ctrl Pts',(16.6533161529773,-19.3449329706041,
6.28915476773769));
#173366=CARTESIAN_POINT('Ctrl Pts',(16.6619704192879,-19.3882734790275,
6.28642560721673));
#173367=CARTESIAN_POINT('Ctrl Pts',(16.681085743994,-19.4705091403054,6.28113243164965));
#173368=CARTESIAN_POINT('Ctrl Pts',(16.6913131117228,-19.5094393553305,
6.27857651366147));
#173369=CARTESIAN_POINT('Ctrl Pts',(16.7452404049068,-19.693224414201,6.26627806706897));
#173370=CARTESIAN_POINT('Ctrl Pts',(16.8032757919129,-19.833405046162,6.25616035700209));
#173371=CARTESIAN_POINT('Ctrl Pts',(16.9019242599444,-20.0141554369697,
6.24267850398749));
#173372=CARTESIAN_POINT('Ctrl Pts',(16.929955191671,-20.0610982082332,6.23913809436873));
#173373=CARTESIAN_POINT('Ctrl Pts',(16.9751922023063,-20.1305936367556,
6.23389087200403));
#173374=CARTESIAN_POINT('Ctrl Pts',(16.991084804231,-20.1539711440418,6.23212480632293));
#173375=CARTESIAN_POINT('Ctrl Pts',(17.0114495429772,-20.182673349827,6.22996217357871));
#173376=CARTESIAN_POINT('Ctrl Pts',(17.0154851701229,-20.1883024522825,
6.22953831573068));
#173377=CARTESIAN_POINT('Ctrl Pts',(17.0219186703776,-20.1971838601842,
6.22887014442115));
#173378=CARTESIAN_POINT('Ctrl Pts',(17.0242983117426,-20.2004492231188,
6.22862460723963));
#173379=CARTESIAN_POINT('Ctrl Pts',(17.0288065179394,-20.2065983561217,
6.22816249371857));
#173380=CARTESIAN_POINT('Ctrl Pts',(17.0309330312536,-20.2094834975402,
6.22794578807074));
#173381=CARTESIAN_POINT('Ctrl Pts',(17.0358149821053,-20.2160719723384,
6.22745116515522));
#173382=CARTESIAN_POINT('Ctrl Pts',(17.0385752081386,-20.2197716996052,
6.22717358598846));
#173383=CARTESIAN_POINT('Ctrl Pts',(17.0459422768841,-20.2295792148904,
6.22643813489804));
#173384=CARTESIAN_POINT('Ctrl Pts',(17.0505702126507,-20.2356711736097,
6.22598169817505));
#173385=CARTESIAN_POINT('Ctrl Pts',(17.0834118429753,-20.2784190071789,
6.22278055155043));
#173386=CARTESIAN_POINT('Ctrl Pts',(17.112789510265,-20.3141695511646,6.22011224294324));
#173387=CARTESIAN_POINT('Ctrl Pts',(17.1681251004714,-20.377180061586,6.21536677188298));
#173388=CARTESIAN_POINT('Ctrl Pts',(17.1936820139472,-20.4047639650173,
6.21327339968138));
#173389=CARTESIAN_POINT('Ctrl Pts',(17.2454134775468,-20.4576976075686,
6.20919107428181));
#173390=CARTESIAN_POINT('Ctrl Pts',(17.271534277295,-20.4830810677156,6.20720160430701));
#173391=CARTESIAN_POINT('Ctrl Pts',(17.3785990815193,-20.5818825497916,
6.1992701886771));
#173392=CARTESIAN_POINT('Ctrl Pts',(17.4645168941252,-20.649657364387,6.19338603766223));
#173393=CARTESIAN_POINT('Ctrl Pts',(17.6009752904639,-20.7411256077791,
6.18425085872232));
#173394=CARTESIAN_POINT('Ctrl Pts',(17.6478458904249,-20.7699615069063,
6.18114859054433));
#173395=CARTESIAN_POINT('Ctrl Pts',(17.7156177725683,-20.8080992950845,
6.17667442661243));
#173396=CARTESIAN_POINT('Ctrl Pts',(17.7356297280632,-20.8189396610462,
6.17535475344012));
#173397=CARTESIAN_POINT('Ctrl Pts',(17.7711481074409,-20.8374453782201,
6.17301265653074));
#173398=CARTESIAN_POINT('Ctrl Pts',(17.7865811598294,-20.8452473573717,
6.17199504449517));
#173399=CARTESIAN_POINT('Ctrl Pts',(17.8094981274425,-20.8564823529428,
6.17048330742093));
#173400=CARTESIAN_POINT('Ctrl Pts',(17.8169095110432,-20.8600623095636,
6.16999431049844));
#173401=CARTESIAN_POINT('Ctrl Pts',(17.8298642262263,-20.8662269744544,
6.16913931828668));
#173402=CARTESIAN_POINT('Ctrl Pts',(17.8353982661557,-20.868831064509,6.16877400061096));
#173403=CARTESIAN_POINT('Ctrl Pts',(17.8464424480703,-20.8739696607753,
6.16804475200748));
#173404=CARTESIAN_POINT('Ctrl Pts',(17.8519523521697,-20.8765045416145,
6.1676808383766));
#173405=CARTESIAN_POINT('Ctrl Pts',(17.8651280114369,-20.8824976535387,
6.16681036374622));
#173406=CARTESIAN_POINT('Ctrl Pts',(17.8728035858138,-20.8859339326431,
6.16630305367577));
#173407=CARTESIAN_POINT('Ctrl Pts',(17.900446064772,-20.8981120038595,6.16447517593854));
#173408=CARTESIAN_POINT('Ctrl Pts',(17.920526696827,-20.9065908072475,6.16314568322973));
#173409=CARTESIAN_POINT('Ctrl Pts',(18.1155344023314,-20.9854048941387,
6.15021472296584));
#173410=CARTESIAN_POINT('Ctrl Pts',(18.2989582507223,-21.032371339003,6.13778451101057));
#173411=CARTESIAN_POINT('Ctrl Pts',(18.5638257376764,-21.0635992777619,
6.12018172853438));
#173412=CARTESIAN_POINT('Ctrl Pts',(18.641983042084,-21.0684463904165,6.11504564636913));
#173413=CARTESIAN_POINT('Ctrl Pts',(18.7557447730535,-21.0691861622347,
6.10779693945435));
#173414=CARTESIAN_POINT('Ctrl Pts',(18.7912584058533,-21.0685235410227,
6.10556662027387));
#173415=CARTESIAN_POINT('Ctrl Pts',(18.8341683241406,-21.0666419508439,
6.10292434407441));
#173416=CARTESIAN_POINT('Ctrl Pts',(18.8415941572181,-21.0662771281299,
6.10246898963634));
#173417=CARTESIAN_POINT('Ctrl Pts',(18.8531643015383,-21.0656475845377,
6.10176264131586));
#173418=CARTESIAN_POINT('Ctrl Pts',(18.8573099317897,-21.0654097813223,
6.10151018176803));
#173419=CARTESIAN_POINT('Ctrl Pts',(18.8650149715528,-21.0649450531459,
6.10104216361974));
#173420=CARTESIAN_POINT('Ctrl Pts',(18.8685744727273,-21.0647213332441,
6.10082643377388));
#173421=CARTESIAN_POINT('Ctrl Pts',(18.8766436548562,-21.0641936976585,
6.10033846292882));
#173422=CARTESIAN_POINT('Ctrl Pts',(18.8811529268464,-21.0638843353011,
6.10006653039827));
#173423=CARTESIAN_POINT('Ctrl Pts',(18.8928092632662,-21.0630471278457,
6.09936547486492));
#173424=CARTESIAN_POINT('Ctrl Pts',(18.899954767083,-21.0624974239907,6.09893754799677));
#173425=CARTESIAN_POINT('Ctrl Pts',(18.9441612624284,-21.0588707163678,
6.09630070388491));
#173426=CARTESIAN_POINT('Ctrl Pts',(18.9811410832951,-21.0548536884396,
6.09414092412532));
#173427=CARTESIAN_POINT('Ctrl Pts',(19.1867552431878,-21.0270186771987,
6.08229475508146));
#173428=CARTESIAN_POINT('Ctrl Pts',(19.3521537696724,-20.9838926253637,
6.07333414141544));
#173429=CARTESIAN_POINT('Ctrl Pts',(19.5990582330958,-20.8865291080759,
6.05873241540789));
#173430=CARTESIAN_POINT('Ctrl Pts',(19.6850469190682,-20.8457358116979,
6.05340058994421));
#173431=CARTESIAN_POINT('Ctrl Pts',(19.7866309135426,-20.7888759189048,
6.04662151622879));
#173432=CARTESIAN_POINT('Ctrl Pts',(19.8051048928457,-20.7781651735305,
6.04536850629302));
#173433=CARTESIAN_POINT('Ctrl Pts',(19.8311329972267,-20.762543909398,6.04357282918225));
#173434=CARTESIAN_POINT('Ctrl Pts',(19.838823056954,-20.7578615867422,6.04303847120485));
#173435=CARTESIAN_POINT('Ctrl Pts',(19.8520345748599,-20.7497013846639,
6.04211372413928));
#173436=CARTESIAN_POINT('Ctrl Pts',(19.8575702922207,-20.7462467433365,
6.04172419405976));
#173437=CARTESIAN_POINT('Ctrl Pts',(19.8681366691222,-20.7395845744625,
6.04097668914648));
#173438=CARTESIAN_POINT('Ctrl Pts',(19.8731699215115,-20.7363812608003,
6.04061887319687));
#173439=CARTESIAN_POINT('Ctrl Pts',(19.8862180549583,-20.7279993271395,
6.03968669117099));
#173440=CARTESIAN_POINT('Ctrl Pts',(19.8942115166272,-20.7227877592174,
6.03911109901927));
#173441=CARTESIAN_POINT('Ctrl Pts',(19.9213240105203,-20.7048486013623,
6.03714312929067));
#173442=CARTESIAN_POINT('Ctrl Pts',(19.9402705076473,-20.6918643402368,
6.03574112578493));
#173443=CARTESIAN_POINT('Ctrl Pts',(20.1024104767653,-20.5768263487607,
6.02350465632215));
#173444=CARTESIAN_POINT('Ctrl Pts',(20.2325583640737,-20.4576251699998,
6.01196334054752));
#173445=CARTESIAN_POINT('Ctrl Pts',(20.402675028537,-20.2576574616752,5.99461738879427));
#173446=CARTESIAN_POINT('Ctrl Pts',(20.4547854833156,-20.1881702913624,
5.98889944139805));
#173447=CARTESIAN_POINT('Ctrl Pts',(20.5232432545789,-20.0841322743137,
5.98094848913989));
#173448=CARTESIAN_POINT('Ctrl Pts',(20.5431537418779,-20.0520354799077,
5.97857330402471));
#173449=CARTESIAN_POINT('Ctrl Pts',(20.5660122068564,-20.0128852679587,
5.97578361078896));
#173450=CARTESIAN_POINT('Ctrl Pts',(20.5697931969881,-20.0063289902624,
5.97531997647551));
#173451=CARTESIAN_POINT('Ctrl Pts',(20.5756085244748,-19.9961190197423,
5.97460361754594));
#173452=CARTESIAN_POINT('Ctrl Pts',(20.5776672888977,-19.9924794151507,
5.97434936064464));
#173453=CARTESIAN_POINT('Ctrl Pts',(20.5814606986839,-19.9857265922021,
5.97387970186458));
#173454=CARTESIAN_POINT('Ctrl Pts',(20.5831982516336,-19.982615120722,5.97366411811812));
#173455=CARTESIAN_POINT('Ctrl Pts',(20.5871028301655,-19.9755814474733,
5.97317861201329));
#173456=CARTESIAN_POINT('Ctrl Pts',(20.5892652587948,-19.971656755549,5.97290898499985));
#173457=CARTESIAN_POINT('Ctrl Pts',(20.5955940859986,-19.9600834872905,
5.97211756886456));
#173458=CARTESIAN_POINT('Ctrl Pts',(20.5997258220393,-19.9524159241269,
5.97159793801832));
#173459=CARTESIAN_POINT('Ctrl Pts',(20.6287422339887,-19.8977630282585,
5.96792583736771));
#173460=CARTESIAN_POINT('Ctrl Pts',(20.6518986191712,-19.8498762364502,
5.96487407255763));
#173461=CARTESIAN_POINT('Ctrl Pts',(20.6798587385253,-19.7860239503508,
5.96095337059357));
#173462=CARTESIAN_POINT('Ctrl Pts',(20.6863110483281,-19.7708063083639,
5.96002974072647));
#173463=CARTESIAN_POINT('Ctrl Pts',(20.7492249714697,-19.617452190958,5.95081513922359));
#173464=CARTESIAN_POINT('Ctrl Pts',(20.7911099715278,-19.4737858125974,
5.94290576256185));
#173465=CARTESIAN_POINT('Ctrl Pts',(20.828449987223,-19.2662674724425,5.93123962701694));
#173466=CARTESIAN_POINT('Ctrl Pts',(20.8367077414126,-19.2051878649734,
5.92778193483492));
#173467=CARTESIAN_POINT('Ctrl Pts',(20.8456586459258,-19.1068179851342,
5.92211297374943));
#173468=CARTESIAN_POINT('Ctrl Pts',(20.8480513818264,-19.0697172561207,
5.91995250223802));
#173469=CARTESIAN_POINT('Ctrl Pts',(20.8498895438205,-19.0214566160792,
5.9171055593353));
#173470=CARTESIAN_POINT('Ctrl Pts',(20.8502253424791,-19.010335888353,5.9164470298258));
#173471=CARTESIAN_POINT('Ctrl Pts',(20.8506288613221,-18.9922469400273,
5.9153715970044));
#173472=CARTESIAN_POINT('Ctrl Pts',(20.8507498648743,-18.9852800320589,
5.91495636757392));
#173473=CARTESIAN_POINT('Ctrl Pts',(20.8509164090886,-18.9718816868263,
5.91415579336967));
#173474=CARTESIAN_POINT('Ctrl Pts',(20.8509670404518,-18.9654503815805,
5.91377061271823));
#173475=CARTESIAN_POINT('Ctrl Pts',(20.8510158622387,-18.9507253274372,
5.91288660615498));
#173476=CARTESIAN_POINT('Ctrl Pts',(20.8509946219938,-18.9424316588326,
5.912387176615));
#173477=CARTESIAN_POINT('Ctrl Pts',(20.850808734445,-18.9204005765702,5.91105635887353));
#173478=CARTESIAN_POINT('Ctrl Pts',(20.8505590980706,-18.9066644489074,
5.91022232399389));
#173479=CARTESIAN_POINT('Ctrl Pts',(20.8476401951111,-18.8020916013823,
5.90383923571801));
#173480=CARTESIAN_POINT('Ctrl Pts',(20.8392585059012,-18.7115208313588,
5.89811144914314));
#173481=CARTESIAN_POINT('Ctrl Pts',(20.8031525277393,-18.4828845147944,
5.8831624275689));
#173482=CARTESIAN_POINT('Ctrl Pts',(20.7674349599478,-18.3465259255292,
5.87376393638202));
#173483=CARTESIAN_POINT('Ctrl Pts',(20.6996503153591,-18.1640735105363,
5.86102482119008));
#173484=CARTESIAN_POINT('Ctrl Pts',(20.6788961788204,-18.1141521829133,
5.85752537179799));
#173485=CARTESIAN_POINT('Ctrl Pts',(20.644500042845,-18.0396044967632,5.85233124189623));
#173486=CARTESIAN_POINT('Ctrl Pts',(20.6322413511948,-18.0143668533074,
5.85057860870479));
#173487=CARTESIAN_POINT('Ctrl Pts',(20.6163422646763,-17.9832253430069,
5.84843003952564));
#173488=CARTESIAN_POINT('Ctrl Pts',(20.613170413408,-17.977087030637,5.84800722677176));
#173489=CARTESIAN_POINT('Ctrl Pts',(20.60809789318,-17.9673871921274,5.84734032449112));
#173490=CARTESIAN_POINT('Ctrl Pts',(20.6062170239817,-17.9638154472006,
5.84709501896253));
#173491=CARTESIAN_POINT('Ctrl Pts',(20.6026464636024,-17.9570817891174,
5.84663308968833));
#173492=CARTESIAN_POINT('Ctrl Pts',(20.6009589780553,-17.9539188275942,
5.8464163380719));
#173493=CARTESIAN_POINT('Ctrl Pts',(20.5970773163752,-17.9466874721828,
5.84592128754615));
#173494=CARTESIAN_POINT('Ctrl Pts',(20.5948778473299,-17.9426219718941,
5.84564332884129));
#173495=CARTESIAN_POINT('Ctrl Pts',(20.5889923492203,-17.9318278358562,
5.84490620685704));
#173496=CARTESIAN_POINT('Ctrl Pts',(20.5852829899473,-17.9251119071071,
5.84444848916911));
#173497=CARTESIAN_POINT('Ctrl Pts',(20.558735100005,-17.8776573982688,5.84121965665632));
#173498=CARTESIAN_POINT('Ctrl Pts',(20.5345886285815,-17.8376609530344,
5.83852643934218));
#173499=CARTESIAN_POINT('Ctrl Pts',(20.5067023993536,-17.7947467154586,
5.83563149080974));
#173500=CARTESIAN_POINT('Ctrl Pts',(20.5042561239897,-17.7910080890895,
5.83537924307333));
#173501=CARTESIAN_POINT('Ctrl Pts',(20.4889651681,-17.7677997155497,5.83381290499945));
#173502=CARTESIAN_POINT('Ctrl Pts',(20.4758109573607,-17.7485351274904,
5.83251073514876));
#173503=CARTESIAN_POINT('Ctrl Pts',(20.4360626303147,-17.6923403059282,
5.82869450340581));
#173504=CARTESIAN_POINT('Ctrl Pts',(20.4085927281712,-17.6560450739698,
5.82620627250336));
#173505=CARTESIAN_POINT('Ctrl Pts',(20.3112069239627,-17.5356439945393,
5.81777526838908));
#173506=CARTESIAN_POINT('Ctrl Pts',(20.2359569921626,-17.4560821128771,
5.81188725839029));
#173507=CARTESIAN_POINT('Ctrl Pts',(20.1140504529712,-17.3457040596506,
5.80274310867441));
#173508=CARTESIAN_POINT('Ctrl Pts',(20.0717732879441,-17.3103277167841,
5.79963569920776));
#173509=CARTESIAN_POINT('Ctrl Pts',(20.0010165637319,-17.2556701441101,
5.79449184930673));
#173510=CARTESIAN_POINT('Ctrl Pts',(19.9733622396418,-17.235361716865,5.79249479329015));
#173511=CARTESIAN_POINT('Ctrl Pts',(19.9363629060227,-17.2095507833398,
5.78983420999984));
#173512=CARTESIAN_POINT('Ctrl Pts',(19.9274509160678,-17.2034346638465,
5.78919420960976));
#173513=CARTESIAN_POINT('Ctrl Pts',(19.912775273546,-17.1935275268055,5.78814151006629));
#173514=CARTESIAN_POINT('Ctrl Pts',(19.9070391663069,-17.1896959124247,
5.78773035215526));
#173515=CARTESIAN_POINT('Ctrl Pts',(19.8958978645778,-17.1823322223919,
5.78693228439748));
#173516=CARTESIAN_POINT('Ctrl Pts',(19.8904950300019,-17.1787967023032,
5.78654550991818));
#173517=CARTESIAN_POINT('Ctrl Pts',(19.8779803887895,-17.1706888667593,
5.78565012623694));
#173518=CARTESIAN_POINT('Ctrl Pts',(19.8708572318772,-17.166134351517,5.7851408608827));
#173519=CARTESIAN_POINT('Ctrl Pts',(19.8516216673883,-17.1539969362302,
5.78376653125884));
#173520=CARTESIAN_POINT('Ctrl Pts',(19.8394596088827,-17.1464939085806,
5.78289853878201));
#173521=CARTESIAN_POINT('Ctrl Pts',(19.7271457697577,-17.0787653843559,
5.77489023814325));
#173522=CARTESIAN_POINT('Ctrl Pts',(19.6222601056303,-17.0268162113851,
5.76744806231527));
#173523=CARTESIAN_POINT('Ctrl Pts',(19.3623098138836,-16.9238457041456,
5.74918452666127));
#173524=CARTESIAN_POINT('Ctrl Pts',(19.2045757370591,-16.8815552105659,
5.73822299193626));
#173525=CARTESIAN_POINT('Ctrl Pts',(19.0114504404594,-16.8530089384606,
5.72581868616253));
#173526=CARTESIAN_POINT('Ctrl Pts',(18.9792388897572,-16.8490020500259,
5.72378472823888));
#173527=CARTESIAN_POINT('Ctrl Pts',(18.9397467944933,-16.84500934631,5.72134388951952));
#173528=CARTESIAN_POINT('Ctrl Pts',(18.932543794116,-16.8443184008294,5.72090084672935));
#173529=CARTESIAN_POINT('Ctrl Pts',(18.9212452374452,-16.8432930256369,
5.72020940423208));
#173530=CARTESIAN_POINT('Ctrl Pts',(18.9171520881604,-16.8429335724214,
5.71995963559178));
#173531=CARTESIAN_POINT('Ctrl Pts',(18.9094986752622,-16.8422839114739,
5.71949399708822));
#173532=CARTESIAN_POINT('Ctrl Pts',(18.9059387629808,-16.8419908006791,
5.71927797207067));
#173533=CARTESIAN_POINT('Ctrl Pts',(18.8978099901034,-16.8413422145912,
5.71878596290514));
#173534=CARTESIAN_POINT('Ctrl Pts',(18.8932407152944,-16.8409925638542,
5.71851030834989));
#173535=CARTESIAN_POINT('Ctrl Pts',(18.8791899348779,-16.8399632478783,
5.71766535145905));
#173536=CARTESIAN_POINT('Ctrl Pts',(18.8697048075751,-16.8393325930649,
5.71709872747489));
#173537=CARTESIAN_POINT('Ctrl Pts',(18.7843129931441,-16.8342324600796,
5.7120289470986));
#173538=CARTESIAN_POINT('Ctrl Pts',(18.7082123316671,-16.8337912368566,
5.70773298215973));
#173539=CARTESIAN_POINT('Ctrl Pts',(18.5898209498408,-16.8394883700714,
5.70117337088389));
#173540=CARTESIAN_POINT('Ctrl Pts',(18.547466633118,-16.8428062037057,5.69885161600951));
#173541=CARTESIAN_POINT('Ctrl Pts',(18.3965609963475,-16.859208907409,5.69058744196724));
#173542=CARTESIAN_POINT('Ctrl Pts',(18.288961472109,-16.8794220256274,5.68470085914685));
#173543=CARTESIAN_POINT('Ctrl Pts',(18.1302307474953,-16.9221761859047,
5.6755600273208));
#173544=CARTESIAN_POINT('Ctrl Pts',(18.0776354836409,-16.9385683513123,
5.6724545195517));
#173545=CARTESIAN_POINT('Ctrl Pts',(17.9934267966454,-16.9684637154784,
5.66731353701058));
#173546=CARTESIAN_POINT('Ctrl Pts',(17.9613969278722,-16.9807189043255,
5.66531738910068));
#173547=CARTESIAN_POINT('Ctrl Pts',(17.919683474215,-16.9978520049024,5.66265784421248));
#173548=CARTESIAN_POINT('Ctrl Pts',(17.909718596724,-17.0020343714392,5.66201795068399));
#173549=CARTESIAN_POINT('Ctrl Pts',(17.8934466830099,-17.0090108851905,
5.66096538213877));
#173550=CARTESIAN_POINT('Ctrl Pts',(17.8871204303578,-17.0117599190403,
5.66055424761143));
#173551=CARTESIAN_POINT('Ctrl Pts',(17.8748983876208,-17.0171420950068,
5.65975619323664));
#173552=CARTESIAN_POINT('Ctrl Pts',(17.8690009808611,-17.0197713933484,
5.6593694085872));
#173553=CARTESIAN_POINT('Ctrl Pts',(17.8554086029071,-17.0259061141775,
5.65847395472911));
#173554=CARTESIAN_POINT('Ctrl Pts',(17.8477224595356,-17.0294307247653,
5.65796462904438));
#173555=CARTESIAN_POINT('Ctrl Pts',(17.8271010189593,-17.0390369725575,
5.65659003103985));
#173556=CARTESIAN_POINT('Ctrl Pts',(17.8142060315361,-17.0452036432742,
5.65572182873334));
#173557=CARTESIAN_POINT('Ctrl Pts',(17.696226356622,-17.1030993784689,5.64769731498152));
#173558=CARTESIAN_POINT('Ctrl Pts',(17.5955588130439,-17.1633269032491,
5.64023771614866));
#173559=CARTESIAN_POINT('Ctrl Pts',(17.3674343851142,-17.3268979014458,
5.62190024953151));
#173560=CARTESIAN_POINT('Ctrl Pts',(17.2459727153523,-17.4373272888777,
5.61087998701859));
#173561=CARTESIAN_POINT('Ctrl Pts',(17.1177578285452,-17.5843594953859,
5.59849616104893));
#173562=CARTESIAN_POINT('Ctrl Pts',(17.0976054366513,-17.6085371665684,
5.59652525315303));
#173563=CARTESIAN_POINT('Ctrl Pts',(17.073533379214,-17.6387631700887,5.59414952095432));
#173564=CARTESIAN_POINT('Ctrl Pts',(17.0690967400017,-17.6443924486247,
5.59371072714514));
#173565=CARTESIAN_POINT('Ctrl Pts',(17.0621710439961,-17.6532722761588,
5.59302443430166));
#173566=CARTESIAN_POINT('Ctrl Pts',(17.0596627288536,-17.6565076372618,
5.59277559907393));
#173567=CARTESIAN_POINT('Ctrl Pts',(17.0549819911819,-17.662581409482,5.59231076245265));
#173568=CARTESIAN_POINT('Ctrl Pts',(17.0528073968767,-17.665418013911,5.59209461154477));
#173569=CARTESIAN_POINT('Ctrl Pts',(17.0478470428556,-17.6719224953121,
5.59160109431123));
#173570=CARTESIAN_POINT('Ctrl Pts',(17.0450660668932,-17.6755939582505,
5.59132406536616));
#173571=CARTESIAN_POINT('Ctrl Pts',(17.0378180122053,-17.6852280509601,
5.59060105794398));
#173572=CARTESIAN_POINT('Ctrl Pts',(17.0333703441385,-17.6912052966883,
5.59015640342551));
#173573=CARTESIAN_POINT('Ctrl Pts',(17.0039154241879,-17.7312293850776,
5.58720407982091));
#173574=CARTESIAN_POINT('Ctrl Pts',(16.9798986668736,-17.7659972236289,
5.58476001796528));
#173575=CARTESIAN_POINT('Ctrl Pts',(16.9164817125184,-17.8639479554217,
5.57813172056542));
#173576=CARTESIAN_POINT('Ctrl Pts',(16.8793476037037,-17.928527502961,5.57404405300756));
#173577=CARTESIAN_POINT('Ctrl Pts',(16.8077026002861,-18.0698842851205,
5.56540885297391));
#173578=CARTESIAN_POINT('Ctrl Pts',(16.7742225791892,-18.1470070983212,
5.56087765657378));
#173579=CARTESIAN_POINT('Ctrl Pts',(16.7454193466937,-18.2258898256491,
5.55626851740655));
#173580=CARTESIAN_POINT('',(16.6170004656572,-18.950595866038,6.0890562790225));
#173581=CARTESIAN_POINT('Ctrl Pts',(16.7454193844609,-18.2258897222169,
5.33540091855303));
#173582=CARTESIAN_POINT('Ctrl Pts',(16.754433949033,-18.2012017527527,5.33706788824166));
#173583=CARTESIAN_POINT('Ctrl Pts',(16.7639100417315,-18.1766767755762,
5.33871640463477));
#173584=CARTESIAN_POINT('Ctrl Pts',(16.7775028833961,-18.1433580018566,
5.34093968279766));
#173585=CARTESIAN_POINT('Ctrl Pts',(16.7812238464402,-18.1344132151779,
5.34153491144854));
#173586=CARTESIAN_POINT('Ctrl Pts',(16.7868091135376,-18.1212425274892,
5.34240859319378));
#173587=CARTESIAN_POINT('Ctrl Pts',(16.788625993279,-18.1169968255376,5.34268980745089));
#173588=CARTESIAN_POINT('Ctrl Pts',(16.7918742109987,-18.1094745084244,
5.34318724763144));
#173589=CARTESIAN_POINT('Ctrl Pts',(16.7932999700237,-18.1061955435284,
5.34340380796438));
#173590=CARTESIAN_POINT('Ctrl Pts',(16.7963728336157,-18.0991772406288,
5.3438667388128));
#173591=CARTESIAN_POINT('Ctrl Pts',(16.7980224537718,-18.0954390646537,
5.34411295281316));
#173592=CARTESIAN_POINT('Ctrl Pts',(16.802581091417,-18.0851892579945,5.34478713183788));
#173593=CARTESIAN_POINT('Ctrl Pts',(16.8055122379532,-18.0786874455159,
5.34521376302037));
#173594=CARTESIAN_POINT('Ctrl Pts',(16.8213484050857,-18.0440285090467,
5.34748314738849));
#173595=CARTESIAN_POINT('Ctrl Pts',(16.8348380680208,-18.0161407498361,
5.34929205450183));
#173596=CARTESIAN_POINT('Ctrl Pts',(16.9233519448441,-17.8429551722759,
5.36047870226354));
#173597=CARTESIAN_POINT('Ctrl Pts',(17.0143947010761,-17.7064492099266,
5.36912121828694));
#173598=CARTESIAN_POINT('Ctrl Pts',(17.1964660723114,-17.4920196930226,
5.38451635750169));
#173599=CARTESIAN_POINT('Ctrl Pts',(17.2800215745483,-17.408790855096,5.39108660895357));
#173600=CARTESIAN_POINT('Ctrl Pts',(17.3809923330986,-17.323729818445,5.39882093143983));
#173601=CARTESIAN_POINT('Ctrl Pts',(17.3920227743658,-17.3146269081943,
5.39966310887849));
#173602=CARTESIAN_POINT('Ctrl Pts',(17.4097221163854,-17.3003194541485,
5.40101055987238));
#173603=CARTESIAN_POINT('Ctrl Pts',(17.41633156251,-17.2950418157808,5.40151288620035));
#173604=CARTESIAN_POINT('Ctrl Pts',(17.4280424976652,-17.2858050234679,
5.40240152660719));
#173605=CARTESIAN_POINT('Ctrl Pts',(17.4331308359691,-17.2818293157964,
5.40278717356146));
#173606=CARTESIAN_POINT('Ctrl Pts',(17.4436912485878,-17.2736556097667,
5.40358663896818));
#173607=CARTESIAN_POINT('Ctrl Pts',(17.449165801305,-17.2694609525151,5.40400058321099));
#173608=CARTESIAN_POINT('Ctrl Pts',(17.4632677460002,-17.2587648602399,
5.40506563981983));
#173609=CARTESIAN_POINT('Ctrl Pts',(17.4719245038197,-17.2523026342785,
5.40571827917524));
#173610=CARTESIAN_POINT('Ctrl Pts',(17.5082358074039,-17.2256267779826,
5.40845127344328));
#173611=CARTESIAN_POINT('Ctrl Pts',(17.5363281837713,-17.2060205147779,
5.4105548943404));
#173612=CARTESIAN_POINT('Ctrl Pts',(17.6107287412886,-17.1567354307796,
5.41610184893497));
#173613=CARTESIAN_POINT('Ctrl Pts',(17.6577374024471,-17.1281657972743,
5.41958343856949));
#173614=CARTESIAN_POINT('Ctrl Pts',(17.8013463570321,-17.0483736930509,
5.43014241484471));
#173615=CARTESIAN_POINT('Ctrl Pts',(17.900852237189,-17.0027700825176,5.43736822709063));
#173616=CARTESIAN_POINT('Ctrl Pts',(18.0393905078837,-16.9518312356504,
5.44711888988099));
#173617=CARTESIAN_POINT('Ctrl Pts',(18.0757095445325,-16.9395857263662,
5.44964641887755));
#173618=CARTESIAN_POINT('Ctrl Pts',(18.1433564257909,-16.9188050095241,
5.45428269774576));
#173619=CARTESIAN_POINT('Ctrl Pts',(18.1745873804996,-16.9099913405522,
5.45639562427383));
#173620=CARTESIAN_POINT('Ctrl Pts',(18.2118426580303,-16.900396482765,5.45887513073604));
#173621=CARTESIAN_POINT('Ctrl Pts',(18.2176821772654,-16.8989190983179,
5.45926259046659));
#173622=CARTESIAN_POINT('Ctrl Pts',(18.2659510721549,-16.8869261459276,
5.46245510065301));
#173623=CARTESIAN_POINT('Ctrl Pts',(18.3086939618794,-16.8777012746337,
5.46521733624854));
#173624=CARTESIAN_POINT('Ctrl Pts',(18.359096822264,-16.8684469671571,5.46837568582161));
#173625=CARTESIAN_POINT('Ctrl Pts',(18.3665059278418,-16.8671274033791,
5.46883746635955));
#173626=CARTESIAN_POINT('Ctrl Pts',(18.378482948755,-16.8650601235504,5.46957975652983));
#173627=CARTESIAN_POINT('Ctrl Pts',(18.3830464792807,-16.8642878433857,
5.46986160625586));
#173628=CARTESIAN_POINT('Ctrl Pts',(18.3911409504078,-16.8629453180559,
5.47035974958842));
#173629=CARTESIAN_POINT('Ctrl Pts',(18.3946708375065,-16.8623690488016,
5.47057638112279));
#173630=CARTESIAN_POINT('Ctrl Pts',(18.4022300915659,-16.8611546278822,
5.47103899954019));
#173631=CARTESIAN_POINT('Ctrl Pts',(18.4062598365983,-16.8605191781447,
5.47128483233343));
#173632=CARTESIAN_POINT('Ctrl Pts',(18.4173105656312,-16.8588093135312,
5.47195689265315));
#173633=CARTESIAN_POINT('Ctrl Pts',(18.424335233447,-16.8577585661216,5.472381800274));
#173634=CARTESIAN_POINT('Ctrl Pts',(18.4616235699675,-16.8523727111395,
5.47462571418014));
#173635=CARTESIAN_POINT('Ctrl Pts',(18.4919748908451,-16.8486579597797,
5.47641176801372));
#173636=CARTESIAN_POINT('Ctrl Pts',(18.5836894513795,-16.8394445994394,
5.48171583979441));
#173637=CARTESIAN_POINT('Ctrl Pts',(18.6452253183669,-16.8359650902674,
5.48515016186904));
#173638=CARTESIAN_POINT('Ctrl Pts',(18.8537589470336,-16.8332884446971,
5.49661962330192));
#173639=CARTESIAN_POINT('Ctrl Pts',(19.0004825832405,-16.8467046089495,
5.504434456642));
#173640=CARTESIAN_POINT('Ctrl Pts',(19.2184209579186,-16.889796715592,5.51683517791733));
#173641=CARTESIAN_POINT('Ctrl Pts',(19.2913689040297,-16.9083062428076,
5.52111972714955));
#173642=CARTESIAN_POINT('Ctrl Pts',(19.3757170650484,-16.9345608256659,
5.52630296666846));
#173643=CARTESIAN_POINT('Ctrl Pts',(19.3882248313633,-16.9385821417002,
5.5270775392275));
#173644=CARTESIAN_POINT('Ctrl Pts',(19.4084805652702,-16.9453031444008,
5.52834198027179));
#173645=CARTESIAN_POINT('Ctrl Pts',(19.4162518112928,-16.9479319456934,
5.52882951243624));
#173646=CARTESIAN_POINT('Ctrl Pts',(19.4300586123929,-16.9526920256414,
5.52970008530443));
#173647=CARTESIAN_POINT('Ctrl Pts',(19.4361001817187,-16.9548056424922,
5.53008253662895));
#173648=CARTESIAN_POINT('Ctrl Pts',(19.448805687718,-16.9593153842814,5.53089005612648));
#173649=CARTESIAN_POINT('Ctrl Pts',(19.4554673613867,-16.9617176096161,
5.53131532358104));
#173650=CARTESIAN_POINT('Ctrl Pts',(19.4730455196085,-16.9681562104988,
5.53244250022741));
#173651=CARTESIAN_POINT('Ctrl Pts',(19.4839408719425,-16.9722492224249,
5.53314629423618));
#173652=CARTESIAN_POINT('Ctrl Pts',(19.5342904522513,-16.9916391118871,
5.53642298330857));
#173653=CARTESIAN_POINT('Ctrl Pts',(19.5733118863955,-17.0080260359025,
5.53903229286097));
#173654=CARTESIAN_POINT('Ctrl Pts',(19.6793107226783,-17.0563264046731,
5.54631991827515));
#173655=CARTESIAN_POINT('Ctrl Pts',(19.7451380104212,-17.0906056811991,
5.55107341881012));
#173656=CARTESIAN_POINT('Ctrl Pts',(19.9379616752512,-17.2042682654032,
5.56565146896423));
#173657=CARTESIAN_POINT('Ctrl Pts',(20.0584676519581,-17.2937258247171,
5.57570072226783));
#173658=CARTESIAN_POINT('Ctrl Pts',(20.173022375557,-17.3992795133665,5.58575053870765));
#173659=CARTESIAN_POINT('Ctrl Pts',(20.1774963120218,-17.403437858724,5.58614384153748));
#173660=CARTESIAN_POINT('Ctrl Pts',(20.2148437594107,-17.4384533105634,
5.58943341140839));
#173661=CARTESIAN_POINT('Ctrl Pts',(20.2467445178454,-17.4703365751843,
5.59228496083212));
#173662=CARTESIAN_POINT('Ctrl Pts',(20.2828016943608,-17.5087536683832,
5.59553267444668));
#173663=CARTESIAN_POINT('Ctrl Pts',(20.2879686611691,-17.5143185101511,
5.59599868237962));
#173664=CARTESIAN_POINT('Ctrl Pts',(20.296216851927,-17.5232982607529,5.59674339828276));
#173665=CARTESIAN_POINT('Ctrl Pts',(20.2993170303833,-17.5266955597187,
5.59702349517267));
#173666=CARTESIAN_POINT('Ctrl Pts',(20.3048120623795,-17.5327567876314,
5.59752025325519));
#173667=CARTESIAN_POINT('Ctrl Pts',(20.3072112524501,-17.5354167207515,
5.59773724043542));
#173668=CARTESIAN_POINT('Ctrl Pts',(20.3123089119801,-17.5410973159954,
5.59819847817065));
#173669=CARTESIAN_POINT('Ctrl Pts',(20.3150054607718,-17.5441196290131,
5.59844258572847));
#173670=CARTESIAN_POINT('Ctrl Pts',(20.3223193026342,-17.5523645520587,
5.59910507398887));
#173671=CARTESIAN_POINT('Ctrl Pts',(20.3269195478702,-17.5576023123404,
5.59952219695394));
#173672=CARTESIAN_POINT('Ctrl Pts',(20.3504126588416,-17.5846191550521,
5.60165522550219));
#173673=CARTESIAN_POINT('Ctrl Pts',(20.3688860507686,-17.606760970648,5.60334192128337));
#173674=CARTESIAN_POINT('Ctrl Pts',(20.4220893071256,-17.6732447468011,
5.60825156091645));
#173675=CARTESIAN_POINT('Ctrl Pts',(20.4555102709456,-17.7186047743925,
5.61140477888345));
#173676=CARTESIAN_POINT('Ctrl Pts',(20.5660785849803,-17.8819374465208,
5.62229126072365));
#173677=CARTESIAN_POINT('Ctrl Pts',(20.6332246192037,-18.0062234101449,
5.62978562537011));
#173678=CARTESIAN_POINT('Ctrl Pts',(20.7212603367996,-18.2170508220902,
5.64245085297522));
#173679=CARTESIAN_POINT('Ctrl Pts',(20.7499480236224,-18.2998459864583,
5.6474083154387));
#173680=CARTESIAN_POINT('Ctrl Pts',(20.7770887500541,-18.39732553729,5.65334122507995));
#173681=CARTESIAN_POINT('Ctrl Pts',(20.7806233643868,-18.4105129812296,
5.65414571868845));
#173682=CARTESIAN_POINT('Ctrl Pts',(20.7860934147498,-18.4317404625099,
5.65544405944733));
#173683=CARTESIAN_POINT('Ctrl Pts',(20.7881097644217,-18.439759390564,5.65593528966799));
#173684=CARTESIAN_POINT('Ctrl Pts',(20.7916099818974,-18.454032652851,5.65681109604792));
#173685=CARTESIAN_POINT('Ctrl Pts',(20.7931124471362,-18.4602823522873,
5.65719506697261));
#173686=CARTESIAN_POINT('Ctrl Pts',(20.7961869752037,-18.4733324787294,
5.65799790573463));
#173687=CARTESIAN_POINT('Ctrl Pts',(20.7977539131636,-18.4801340225174,
5.65841693335104));
#173688=CARTESIAN_POINT('Ctrl Pts',(20.8017429340734,-18.4978490036616,
5.65950992845358));
#173689=CARTESIAN_POINT('Ctrl Pts',(20.8041122353658,-18.5087739917771,
5.66018558039105));
#173690=CARTESIAN_POINT('Ctrl Pts',(20.8140881492265,-18.5565992267383,
5.66315059981171));
#173691=CARTESIAN_POINT('Ctrl Pts',(20.8207950690573,-18.5936781700032,
5.66546845862681));
#173692=CARTESIAN_POINT('Ctrl Pts',(20.8360316170003,-18.6929745094115,
5.67173021859019));
#173693=CARTESIAN_POINT('Ctrl Pts',(20.8427880694131,-18.7554222245571,
5.67572581940703));
#173694=CARTESIAN_POINT('Ctrl Pts',(20.8529257464839,-18.9153491949447,
5.68608641475998));
#173695=CARTESIAN_POINT('Ctrl Pts',(20.8523661267429,-19.0129295550779,
5.69253289499523));
#173696=CARTESIAN_POINT('Ctrl Pts',(20.8362349370176,-19.2283033897917,
5.706799865447));
#173697=CARTESIAN_POINT('Ctrl Pts',(20.8174727821903,-19.3455517733947,
5.71459383377768));
#173698=CARTESIAN_POINT('Ctrl Pts',(20.7867036120705,-19.4698682939201,
5.7225040375181));
#173699=CARTESIAN_POINT('Ctrl Pts',(20.7843532286604,-19.4790970824845,
5.7230890371202));
#173700=CARTESIAN_POINT('Ctrl Pts',(20.780778814449,-19.4927462582499,5.72395061584839));
#173701=CARTESIAN_POINT('Ctrl Pts',(20.7796026042249,-19.497178885863,5.72422984912721));
#173702=CARTESIAN_POINT('Ctrl Pts',(20.7774845626374,-19.5050575046963,
5.72472510748545));
#173703=CARTESIAN_POINT('Ctrl Pts',(20.7765484055392,-19.508504962176,5.72494145599792));
#173704=CARTESIAN_POINT('Ctrl Pts',(20.7745173001035,-19.5159104647103,
5.72540540750867));
#173705=CARTESIAN_POINT('Ctrl Pts',(20.7734195633255,-19.5198676867155,
5.72565284625754));
#173706=CARTESIAN_POINT('Ctrl Pts',(20.7703585804263,-19.530778837324,5.72633384232184));
#173707=CARTESIAN_POINT('Ctrl Pts',(20.7683712149744,-19.5377260227424,
5.72676602051922));
#173708=CARTESIAN_POINT('Ctrl Pts',(20.7573044102899,-19.5756760907432,
5.72911979156386));
#173709=CARTESIAN_POINT('Ctrl Pts',(20.7475512793176,-19.6064800265913,
5.73100448674677));
#173710=CARTESIAN_POINT('Ctrl Pts',(20.6843902247641,-19.7911637499992,
5.7422142041314));
#173711=CARTESIAN_POINT('Ctrl Pts',(20.6140695368678,-19.9386956435286,
5.75082287827826));
#173712=CARTESIAN_POINT('Ctrl Pts',(20.4654105553701,-20.1757533414089,
5.76614094015221));
#173713=CARTESIAN_POINT('Ctrl Pts',(20.3952159709305,-20.2694638448558,
5.77266675538923));
#173714=CARTESIAN_POINT('Ctrl Pts',(20.3081688603013,-20.36758667267,5.78035106190394));
#173715=CARTESIAN_POINT('Ctrl Pts',(20.2985772493002,-20.378180649372,5.7811926253937));
#173716=CARTESIAN_POINT('Ctrl Pts',(20.2831414126377,-20.3948864717692,
5.78253927751728));
#173717=CARTESIAN_POINT('Ctrl Pts',(20.277366453126,-20.4010619293064,5.7830414244519));
#173718=CARTESIAN_POINT('Ctrl Pts',(20.2671163332905,-20.411892119244,5.78392985587015));
#173719=CARTESIAN_POINT('Ctrl Pts',(20.2626565553318,-20.4165613082586,
5.7843154742351));
#173720=CARTESIAN_POINT('Ctrl Pts',(20.253388225888,-20.4261763810269,5.78511498677931));
#173721=CARTESIAN_POINT('Ctrl Pts',(20.2485767269903,-20.4311193054153,
5.78552900727363));
#173722=CARTESIAN_POINT('Ctrl Pts',(20.236164377411,-20.443746629118,5.78659448414575));
#173723=CARTESIAN_POINT('Ctrl Pts',(20.2285287481798,-20.4513964240075,
5.78724746984077));
#173724=CARTESIAN_POINT('Ctrl Pts',(20.1964159784567,-20.483079762904,5.78998381866931));
#173725=CARTESIAN_POINT('Ctrl Pts',(20.1714162057145,-20.5065739511842,
5.79209051929034));
#173726=CARTESIAN_POINT('Ctrl Pts',(20.1047997625853,-20.5661973818843,
5.797647530931));
#173727=CARTESIAN_POINT('Ctrl Pts',(20.0623257470958,-20.6013256396556,
5.80113627107753));
#173728=CARTESIAN_POINT('Ctrl Pts',(19.9315791246987,-20.7011312010865,
5.81170898535592));
#173729=CARTESIAN_POINT('Ctrl Pts',(19.8396173858778,-20.7606631661658,
5.81894133976479));
#173730=CARTESIAN_POINT('Ctrl Pts',(19.6394019071724,-20.8692781744089,
5.83398783200305));
#173731=CARTESIAN_POINT('Ctrl Pts',(19.5307613354876,-20.9169137672831,
5.84177392127846));
#173732=CARTESIAN_POINT('Ctrl Pts',(19.4096763468073,-20.9583004109624,
5.84967776298821));
#173733=CARTESIAN_POINT('Ctrl Pts',(19.4006354689389,-20.9613225286211,
5.85026333632698));
#173734=CARTESIAN_POINT('Ctrl Pts',(19.3872134520778,-20.9657085771535,
5.85112559446481));
#173735=CARTESIAN_POINT('Ctrl Pts',(19.3828479412285,-20.9671194499969,
5.85140493936761));
#173736=CARTESIAN_POINT('Ctrl Pts',(19.3750749369647,-20.9696036993622,
5.85190032024666));
#173737=CARTESIAN_POINT('Ctrl Pts',(19.3716692852213,-20.9706826510944,
5.85211668027456));
#173738=CARTESIAN_POINT('Ctrl Pts',(19.3643440103366,-20.9729829992078,
5.85258057234032));
#173739=CARTESIAN_POINT('Ctrl Pts',(19.360423572214,-20.9742016129177,5.85282794057178));
#173740=CARTESIAN_POINT('Ctrl Pts',(19.3495985006389,-20.9775319346873,
5.85350854369729));
#173741=CARTESIAN_POINT('Ctrl Pts',(19.3426864959403,-20.9796197586094,
5.85394040210108));
#173742=CARTESIAN_POINT('Ctrl Pts',(19.3048668542628,-20.9908326492226,
5.85628920499539));
#173743=CARTESIAN_POINT('Ctrl Pts',(19.2737628175131,-20.9992869590498,
5.8581694353563));
#173744=CARTESIAN_POINT('Ctrl Pts',(19.0843025193898,-21.0461651548016,
5.86937944722153));
#173745=CARTESIAN_POINT('Ctrl Pts',(18.9221230792634,-21.0669139971618,
5.87799151927304));
#173746=CARTESIAN_POINT('Ctrl Pts',(18.6422408361077,-21.0702398331054,
5.89331429267761));
#173747=CARTESIAN_POINT('Ctrl Pts',(18.5254286432224,-21.0619413391152,
5.89984122875645));
#173748=CARTESIAN_POINT('Ctrl Pts',(18.395784578589,-21.0418573073978,5.90752679697457));
#173749=CARTESIAN_POINT('Ctrl Pts',(18.38168468691,-21.0395265607444,5.90836837668167));
#173750=CARTESIAN_POINT('Ctrl Pts',(18.3592822524734,-21.0355899543386,
5.90971504990787));
#173751=CARTESIAN_POINT('Ctrl Pts',(18.350963713911,-21.0340767729619,5.91021720158176));
#173752=CARTESIAN_POINT('Ctrl Pts',(18.3363089495164,-21.0313202061658,
5.91110563852035));
#173753=CARTESIAN_POINT('Ctrl Pts',(18.3299688939879,-21.0300975808063,
5.91149125763992));
#173754=CARTESIAN_POINT('Ctrl Pts',(18.3168673872367,-21.0275088451415,
5.91229076893606));
#173755=CARTESIAN_POINT('Ctrl Pts',(18.3101068289092,-21.0261386551149,
5.91270478741361));
#173756=CARTESIAN_POINT('Ctrl Pts',(18.2927708565883,-21.0225368052788,
5.91377025317083));
#173757=CARTESIAN_POINT('Ctrl Pts',(18.2822057140478,-21.0202571734208,
5.91442322970615));
#173758=CARTESIAN_POINT('Ctrl Pts',(18.2381844207426,-21.0104053430644,
5.91715948976383));
#173759=CARTESIAN_POINT('Ctrl Pts',(18.2048988775109,-21.002101809893,5.91926610888014));
#173760=CARTESIAN_POINT('Ctrl Pts',(18.1187107711583,-20.978362263788,5.9248228542819));
#173761=CARTESIAN_POINT('Ctrl Pts',(18.0661857632456,-20.9616636991741,
5.92831140510364));
#173762=CARTESIAN_POINT('Ctrl Pts',(17.8184621070226,-20.8721238884677,
5.94524253490021));
#173763=CARTESIAN_POINT('Ctrl Pts',(17.6341001355082,-20.7727945402005,
5.95943300876748));
#173764=CARTESIAN_POINT('Ctrl Pts',(17.4635919722165,-20.6454500092709,
5.9728494765435));
#173765=CARTESIAN_POINT('Ctrl Pts',(17.4599738122632,-20.6427296545023,
5.97313425606137));
#173766=CARTESIAN_POINT('Ctrl Pts',(17.4399959671345,-20.6276085398481,
5.97470702139216));
#173767=CARTESIAN_POINT('Ctrl Pts',(17.4238079167231,-20.6149814169334,
5.97598271146736));
#173768=CARTESIAN_POINT('Ctrl Pts',(17.4027810313994,-20.5980821997696,
5.97763860701494));
#173769=CARTESIAN_POINT('Ctrl Pts',(17.3977750251302,-20.5940211234255,
5.97803275146324));
#173770=CARTESIAN_POINT('Ctrl Pts',(17.3897442118159,-20.5874451529167,
5.9786648050546));
#173771=CARTESIAN_POINT('Ctrl Pts',(17.386707774317,-20.5849446198398,5.97890372616249));
#173772=CARTESIAN_POINT('Ctrl Pts',(17.3810359180814,-20.5802472061477,
5.97934987773984));
#173773=CARTESIAN_POINT('Ctrl Pts',(17.3783988701044,-20.5780523817002,
5.97955725067337));
#173774=CARTESIAN_POINT('Ctrl Pts',(17.3721624888226,-20.5728361043561,
5.98004755412945));
#173775=CARTESIAN_POINT('Ctrl Pts',(17.3685678362495,-20.5698090404011,
5.98033007578921));
#173776=CARTESIAN_POINT('Ctrl Pts',(17.3573349183623,-20.5602856700686,
5.98121275390682));
#173777=CARTESIAN_POINT('Ctrl Pts',(17.3497325798042,-20.5537469406319,
5.98180989073701));
#173778=CARTESIAN_POINT('Ctrl Pts',(17.3319067413098,-20.5381933260096,
5.98321024073961));
#173779=CARTESIAN_POINT('Ctrl Pts',(17.3217231634268,-20.5291331365875,
5.9840103878859));
#173780=CARTESIAN_POINT('Ctrl Pts',(17.2863073425746,-20.4970060368439,
5.98679657699121));
#173781=CARTESIAN_POINT('Ctrl Pts',(17.2615458532658,-20.4734258841379,
5.98875091460641));
#173782=CARTESIAN_POINT('Ctrl Pts',(17.1836732754796,-20.3955855636051,
5.99496002785008));
#173783=CARTESIAN_POINT('Ctrl Pts',(17.1329039463589,-20.3390634504074,
5.99910803211691));
#173784=CARTESIAN_POINT('Ctrl Pts',(16.9773656441819,-20.1459517987438,
6.01259282574975));
#173785=CARTESIAN_POINT('Ctrl Pts',(16.8861986189146,-19.9993339378304,
6.02185803999852));
#173786=CARTESIAN_POINT('Ctrl Pts',(16.8039951982117,-19.8222356839923,
6.03320082167258));
#173787=CARTESIAN_POINT('Ctrl Pts',(16.7945621925219,-19.8010050699168,
6.03456160741386));
#173788=CARTESIAN_POINT('Ctrl Pts',(16.7817332890366,-19.7708013035738,
6.03650075742275));
#173789=CARTESIAN_POINT('Ctrl Pts',(16.7780458554122,-19.7619532487414,
6.03706920488626));
#173790=CARTESIAN_POINT('Ctrl Pts',(16.7721580869368,-19.747550750926,6.03799523947808));
#173791=CARTESIAN_POINT('Ctrl Pts',(16.7699209237878,-19.7420114368851,
6.03835157590773));
#173792=CARTESIAN_POINT('Ctrl Pts',(16.7652917997094,-19.7304083201676,
6.03909838999349));
#173793=CARTESIAN_POINT('Ctrl Pts',(16.7629043425996,-19.7243427986974,
6.03948901484956));
#173794=CARTESIAN_POINT('Ctrl Pts',(16.7572996268597,-19.7099083219375,
6.04041919415483));
#173795=CARTESIAN_POINT('Ctrl Pts',(16.7541074665883,-19.7015298138903,
6.04095958430167));
#173796=CARTESIAN_POINT('Ctrl Pts',(16.7435701496583,-19.6733353125818,
6.04277975751818));
#173797=CARTESIAN_POINT('Ctrl Pts',(16.736468697918,-19.6534301595239,6.04406762352146));
#173798=CARTESIAN_POINT('Ctrl Pts',(16.6996529282216,-19.5451404165116,
6.05109143606473));
#173799=CARTESIAN_POINT('Ctrl Pts',(16.6755085000078,-19.4549834205257,
6.05700831957264));
#173800=CARTESIAN_POINT('Ctrl Pts',(16.6304385570067,-19.2275615688264,
6.07205887777749));
#173801=CARTESIAN_POINT('Ctrl Pts',(16.6169140925337,-19.0892811970425,
6.08133516793109));
#173802=CARTESIAN_POINT('Ctrl Pts',(16.6170004105532,-18.9506815606685,
6.09037076557823));
#173803=CARTESIAN_POINT('Ctrl Pts',(16.7454193692319,-18.2258897639242,
6.13370787796071));
#173804=CARTESIAN_POINT('Ctrl Pts',(16.7204253525143,-18.2943402760645,
6.12932687904854));
#173805=CARTESIAN_POINT('Ctrl Pts',(16.6989959006628,-18.3640109059891,
6.12494588013637));
#173806=CARTESIAN_POINT('Ctrl Pts',(16.6812266680874,-18.4344957509464,
6.1205648812242));
#173807=CARTESIAN_POINT('Ctrl Pts',(16.6634283619283,-18.505095921483,6.11617671422876));
#173808=CARTESIAN_POINT('Ctrl Pts',(16.6493023130958,-18.5765124923157,
6.11178854723333));
#173809=CARTESIAN_POINT('Ctrl Pts',(16.6388927520737,-18.6483313982534,
6.1074003802379));
#173810=CARTESIAN_POINT('Ctrl Pts',(16.6365508801238,-18.6644887252465,
6.10641316039488));
#173811=CARTESIAN_POINT('Ctrl Pts',(16.6343969017635,-18.6806664075672,
6.10542594055187));
#173812=CARTESIAN_POINT('Ctrl Pts',(16.6324309574259,-18.6968597262404,
6.10443872070885));
#173813=CARTESIAN_POINT('Ctrl Pts',(16.6222201199426,-18.7809655384568,
6.09931124014674));
#173814=CARTESIAN_POINT('Ctrl Pts',(16.6170567766291,-18.8656963446802,
6.09418375958462));
#173815=CARTESIAN_POINT('Ctrl Pts',(16.6170004656572,-18.950595866038,6.0890562790225));
#173816=CARTESIAN_POINT('Origin',(18.734,-18.952,0.));
#173817=CARTESIAN_POINT('',(16.7454193236514,-18.2258898887545,7.15616137122352));
#173818=CARTESIAN_POINT('',(16.7486737197731,-18.2270709325543,6.93361858681016));
#173819=CARTESIAN_POINT('',(16.7454193692319,-18.2258897639242,0.));
#173820=CARTESIAN_POINT('Ctrl Pts',(16.7454193236514,-18.2258898887546,
7.15616137122351));
#173821=CARTESIAN_POINT('Ctrl Pts',(16.7205840422062,-18.2939056896761,
7.15141136591347));
#173822=CARTESIAN_POINT('Ctrl Pts',(16.6992294961428,-18.3632196084634,
7.14660725207261));
#173823=CARTESIAN_POINT('Ctrl Pts',(16.6631797913716,-18.5059445142713,
7.13689819598514));
#173824=CARTESIAN_POINT('Ctrl Pts',(16.6487382377985,-18.5792443860931,
7.13200642664211));
#173825=CARTESIAN_POINT('Ctrl Pts',(16.6333272121045,-18.6873232098812,
7.12505656814692));
#173826=CARTESIAN_POINT('Ctrl Pts',(16.629291438054,-18.7216043578968,7.12289061591573));
#173827=CARTESIAN_POINT('Ctrl Pts',(16.6254128245581,-18.7633111888787,
7.12031415742816));
#173828=CARTESIAN_POINT('Ctrl Pts',(16.62476854426,-18.770654987178,7.11986269306851));
#173829=CARTESIAN_POINT('Ctrl Pts',(16.6238224665487,-18.7821267945445,
7.11916105190624));
#173830=CARTESIAN_POINT('Ctrl Pts',(16.6234943985693,-18.7862524943738,
7.11890944030274));
#173831=CARTESIAN_POINT('Ctrl Pts',(16.6229060239731,-18.7939368614968,
7.11844218237915));
#173832=CARTESIAN_POINT('Ctrl Pts',(16.6226426179124,-18.7974951886471,
7.11822636985866));
#173833=CARTESIAN_POINT('Ctrl Pts',(16.6220645668247,-18.8055816665784,
7.11773717361678));
#173834=CARTESIAN_POINT('Ctrl Pts',(16.6217554882698,-18.8101101631181,
7.11746410481957));
#173835=CARTESIAN_POINT('Ctrl Pts',(16.6209918950824,-18.8218538767062,
7.11675817189079));
#173836=CARTESIAN_POINT('Ctrl Pts',(16.6205597664585,-18.8290705588811,
7.11632653177196));
#173837=CARTESIAN_POINT('Ctrl Pts',(16.6180743367141,-18.8744751346457,
7.11362364774395));
#173838=CARTESIAN_POINT('Ctrl Pts',(16.6170190194692,-18.9127131790533,
7.11140440706729));
#173839=CARTESIAN_POINT('Ctrl Pts',(16.6169207094652,-19.1130991496786,
7.09997625594565));
#173840=CARTESIAN_POINT('Ctrl Pts',(16.6354677196798,-19.2747232329275,
7.09141461483807));
#173841=CARTESIAN_POINT('Ctrl Pts',(16.697373122891,-19.5402575685224,7.07645434330741));
#173842=CARTESIAN_POINT('Ctrl Pts',(16.7308397027785,-19.6457147643738,
7.07026707766899));
#173843=CARTESIAN_POINT('Ctrl Pts',(16.777712666695,-19.7612157292806,7.06296367776398));
#173844=CARTESIAN_POINT('Ctrl Pts',(16.7831788076353,-19.7743058359248,
7.06212823659863));
#173845=CARTESIAN_POINT('Ctrl Pts',(16.7921001452617,-19.7950806157054,
7.06078955305786));
#173846=CARTESIAN_POINT('Ctrl Pts',(16.7954704367952,-19.802801445616,7.06028919752226));
#173847=CARTESIAN_POINT('Ctrl Pts',(16.8015031073668,-19.8163994371424,
7.05940285044233));
#173848=CARTESIAN_POINT('Ctrl Pts',(16.8041464536137,-19.822284961979,7.05901751498165));
#173849=CARTESIAN_POINT('Ctrl Pts',(16.8096767357639,-19.8344492800026,
7.05821751895034));
#173850=CARTESIAN_POINT('Ctrl Pts',(16.8125675911792,-19.8407261972221,
7.05780272678382));
#173851=CARTESIAN_POINT('Ctrl Pts',(16.82008271323,-19.8568357214004,7.05673299948148));
#173852=CARTESIAN_POINT('Ctrl Pts',(16.8247519979579,-19.8666469937216,
7.05607651141696));
#173853=CARTESIAN_POINT('Ctrl Pts',(16.8446948516566,-19.907733471956,7.05330601284697));
#173854=CARTESIAN_POINT('Ctrl Pts',(16.8606622755661,-19.9386640549607,
7.05116793022875));
#173855=CARTESIAN_POINT('Ctrl Pts',(16.9043949478943,-20.01848702026,7.04550808426069));
#173856=CARTESIAN_POINT('Ctrl Pts',(16.9333567099543,-20.0666892324598,
7.04194609514396));
#173857=CARTESIAN_POINT('Ctrl Pts',(17.033235571777,-20.2188531399357,7.03023623095629));
#173858=CARTESIAN_POINT('Ctrl Pts',(17.1115049696023,-20.3176579849348,
7.02187674911319));
#173859=CARTESIAN_POINT('Ctrl Pts',(17.2668984461352,-20.4814782138005,
7.00699926012126));
#173860=CARTESIAN_POINT('Ctrl Pts',(17.340787624772,-20.5490768939823,7.00047971996934));
#173861=CARTESIAN_POINT('Ctrl Pts',(17.4267853739081,-20.6172245780694,
6.9937003735011));
#173862=CARTESIAN_POINT('Ctrl Pts',(17.434424519406,-20.6231931523665,6.99310474164512));
#173863=CARTESIAN_POINT('Ctrl Pts',(17.4457640290431,-20.6319281000143,
6.99223058323371));
#173864=CARTESIAN_POINT('Ctrl Pts',(17.449432755844,-20.6347350754828,6.99194929125815));
#173865=CARTESIAN_POINT('Ctrl Pts',(17.4559575628414,-20.6396934893593,
6.99145176513152));
#173866=CARTESIAN_POINT('Ctrl Pts',(17.4588099326086,-20.6418497205106,
6.99123519614061));
#173867=CARTESIAN_POINT('Ctrl Pts',(17.464932836444,-20.6464539600509,6.99077230377625));
#173868=CARTESIAN_POINT('Ctrl Pts',(17.4682049880638,-20.6488997250145,
6.99052613662012));
#173869=CARTESIAN_POINT('Ctrl Pts',(17.4772061326084,-20.6555870939352,
6.98985221814885));
#173870=CARTESIAN_POINT('Ctrl Pts',(17.482949561784,-20.6598093031912,6.98942579895779));
#173871=CARTESIAN_POINT('Ctrl Pts',(17.5137221168821,-20.6821928119932,
6.98715956675343));
#173872=CARTESIAN_POINT('Ctrl Pts',(17.5391269999282,-20.6998340938013,
6.98535348852625));
#173873=CARTESIAN_POINT('Ctrl Pts',(17.6171834267134,-20.7515391392161,
6.97996801335136));
#173874=CARTESIAN_POINT('Ctrl Pts',(17.6709725792072,-20.7838281096898,
6.97647536587213));
#173875=CARTESIAN_POINT('Ctrl Pts',(17.8443351482861,-20.8776833556854,
6.96564099390635));
#173876=CARTESIAN_POINT('Ctrl Pts',(17.9683763451223,-20.9302772946545,
6.9584722452433));
#173877=CARTESIAN_POINT('Ctrl Pts',(18.1354765441738,-20.9830399900457,
6.94874720043832));
#173878=CARTESIAN_POINT('Ctrl Pts',(18.17473005089,-20.9941975043606,6.94645996765171));
#173879=CARTESIAN_POINT('Ctrl Pts',(18.2613895347852,-21.0161438868505,
6.94137922699533));
#173880=CARTESIAN_POINT('Ctrl Pts',(18.3088928558736,-21.0264478833089,
6.93857392112183));
#173881=CARTESIAN_POINT('Ctrl Pts',(18.3691073382889,-21.03735397004,6.93497490416398));
#173882=CARTESIAN_POINT('Ctrl Pts',(18.381528146417,-21.0394892615366,6.93423025968309));
#173883=CARTESIAN_POINT('Ctrl Pts',(18.4012400734647,-21.0426970436934,
6.93304465328028));
#173884=CARTESIAN_POINT('Ctrl Pts',(18.4085191234941,-21.0438426074014,
6.93260601410387));
#173885=CARTESIAN_POINT('Ctrl Pts',(18.4220931084109,-21.0459062918154,
6.93178643766937));
#173886=CARTESIAN_POINT('Ctrl Pts',(18.4283865045984,-21.0468340884151,
6.93140581205598));
#173887=CARTESIAN_POINT('Ctrl Pts',(18.4423736272109,-21.0488317520093,
6.93055840763253));
#173888=CARTESIAN_POINT('Ctrl Pts',(18.450069225143,-21.0498876638469,6.93009119252828));
#173889=CARTESIAN_POINT('Ctrl Pts',(18.4724466614918,-21.0528326861058,
6.92872968181976));
#173890=CARTESIAN_POINT('Ctrl Pts',(18.4871424945694,-21.0546101584567,
6.92783187789438));
#173891=CARTESIAN_POINT('Ctrl Pts',(18.6040636645042,-21.0675092078417,
6.92065849927563));
#173892=CARTESIAN_POINT('Ctrl Pts',(18.7069422908414,-21.0713218500874,
6.91415210350628));
#173893=CARTESIAN_POINT('Ctrl Pts',(18.9653712327339,-21.0620776316681,
6.89736585629444));
#173894=CARTESIAN_POINT('Ctrl Pts',(19.1199622063566,-21.0393403449755,
6.88689550539218));
#173895=CARTESIAN_POINT('Ctrl Pts',(19.3214687454626,-20.9865340776092,
6.87343963271799));
#173896=CARTESIAN_POINT('Ctrl Pts',(19.3717748098951,-20.9713297716734,
6.87010191625839));
#173897=CARTESIAN_POINT('Ctrl Pts',(19.4296851682674,-20.9514465840586,
6.86632509219423));
#173898=CARTESIAN_POINT('Ctrl Pts',(19.4378858215163,-20.9485743792971,
6.86579182172744));
#173899=CARTESIAN_POINT('Ctrl Pts',(19.4502843393181,-20.9441460247169,
6.86498819790692));
#173900=CARTESIAN_POINT('Ctrl Pts',(19.4544952188937,-20.9426269562505,
6.86471572579251));
#173901=CARTESIAN_POINT('Ctrl Pts',(19.4620494704452,-20.9398746607746,
6.86422778459499));
#173902=CARTESIAN_POINT('Ctrl Pts',(19.4653945595866,-20.9386463442574,
6.86401202969258));
#173903=CARTESIAN_POINT('Ctrl Pts',(19.472661434878,-20.9359571060101,6.86354400158541));
#173904=CARTESIAN_POINT('Ctrl Pts',(19.4765819827785,-20.9344930046314,
6.86329192125436));
#173905=CARTESIAN_POINT('Ctrl Pts',(19.4875952542926,-20.9303429209852,
6.86258492723344));
#173906=CARTESIAN_POINT('Ctrl Pts',(19.4946780054251,-20.9276304047851,
6.86213157150478));
#173907=CARTESIAN_POINT('Ctrl Pts',(19.537198546351,-20.911083537179,6.85941698078505));
#173908=CARTESIAN_POINT('Ctrl Pts',(19.5722751497765,-20.8963331477928,
6.8572072784303));
#173909=CARTESIAN_POINT('Ctrl Pts',(19.6869983762708,-20.8444074489981,
6.85001917294139));
#173910=CARTESIAN_POINT('Ctrl Pts',(19.7647318453029,-20.8032174828116,
6.84521011970471));
#173911=CARTESIAN_POINT('Ctrl Pts',(19.9882640263207,-20.6663125020235,
6.83095045532758));
#173912=CARTESIAN_POINT('Ctrl Pts',(20.1250238164415,-20.5573322364003,
6.82157749679089));
#173913=CARTESIAN_POINT('Ctrl Pts',(20.2630317539919,-20.4163373137427,
6.81011396583166));
#173914=CARTESIAN_POINT('Ctrl Pts',(20.27890756625,-20.3995781233629,6.80876165751377));
#173915=CARTESIAN_POINT('Ctrl Pts',(20.3009668565588,-20.3755151181416,
6.80683254484499));
#173916=CARTESIAN_POINT('Ctrl Pts',(20.307380096146,-20.36842348527,6.80626551687288));
#173917=CARTESIAN_POINT('Ctrl Pts',(20.317718983374,-20.356834089197,6.80534116612256));
#173918=CARTESIAN_POINT('Ctrl Pts',(20.3216740787798,-20.3523626869192,
6.80498508491906));
#173919=CARTESIAN_POINT('Ctrl Pts',(20.3299107197553,-20.3429710688386,
6.8042382947326));
#173920=CARTESIAN_POINT('Ctrl Pts',(20.3341885394292,-20.3380476819278,
6.8038474362912));
#173921=CARTESIAN_POINT('Ctrl Pts',(20.3443064028859,-20.3262936556785,
6.80291575976586));
#173922=CARTESIAN_POINT('Ctrl Pts',(20.350125802035,-20.3194454838558,6.80237409879659));
#173923=CARTESIAN_POINT('Ctrl Pts',(20.3695621385229,-20.2962757539406,
6.80054519409433));
#173924=CARTESIAN_POINT('Ctrl Pts',(20.3829764782285,-20.2797866297497,
6.79924976134771));
#173925=CARTESIAN_POINT('Ctrl Pts',(20.4545180199004,-20.18909014491,6.792155086083));
#173926=CARTESIAN_POINT('Ctrl Pts',(20.5078803601392,-20.1112750502559,
6.78617079350107));
#173927=CARTESIAN_POINT('Ctrl Pts',(20.6403889128631,-19.8873645819508,
6.76927208601287));
#173928=CARTESIAN_POINT('Ctrl Pts',(20.7078127914036,-19.7351252486921,
6.7580895347162));
#173929=CARTESIAN_POINT('Ctrl Pts',(20.7691591445091,-19.5364487520998,
6.74476058614701));
#173930=CARTESIAN_POINT('Ctrl Pts',(20.7803546805778,-19.4959541821624,
6.74210945345194));
#173931=CARTESIAN_POINT('Ctrl Pts',(20.7921063628785,-19.4479259183983,
6.73906263745244));
#173932=CARTESIAN_POINT('Ctrl Pts',(20.793836006481,-19.4406920785126,6.73860631930271));
#173933=CARTESIAN_POINT('Ctrl Pts',(20.7965740907663,-19.4289678162969,
6.73787108305089));
#173934=CARTESIAN_POINT('Ctrl Pts',(20.7976060584196,-19.4244830306595,
6.73759086485057));
#173935=CARTESIAN_POINT('Ctrl Pts',(20.7994134599979,-19.4165094312379,
6.73709452363717));
#173936=CARTESIAN_POINT('Ctrl Pts',(20.8001946905246,-19.413021988593,6.73687807173217));
#173937=CARTESIAN_POINT('Ctrl Pts',(20.8018523888711,-19.4055331043866,
6.73641463657394));
#173938=CARTESIAN_POINT('Ctrl Pts',(20.8027260732621,-19.4015311039228,
6.73616781369144));
#173939=CARTESIAN_POINT('Ctrl Pts',(20.8050988636786,-19.3905088677092,
6.73549024767434));
#173940=CARTESIAN_POINT('Ctrl Pts',(20.8065739032446,-19.3834834285796,
6.73506086079326));
#173941=CARTESIAN_POINT('Ctrl Pts',(20.8143542752058,-19.3454658179259,
6.73275002415719));
#173942=CARTESIAN_POINT('Ctrl Pts',(20.8200005951603,-19.3143410260219,
6.7309039019925));
#173943=CARTESIAN_POINT('Ctrl Pts',(20.8505124673408,-19.1216535872645,
6.71969131597434));
#173944=CARTESIAN_POINT('Ctrl Pts',(20.8572960747971,-18.9577730278763,
6.71105305100452));
#173945=CARTESIAN_POINT('Ctrl Pts',(20.8364523718367,-18.6779727513606,
6.69569421656281));
#173946=CARTESIAN_POINT('Ctrl Pts',(20.8180853133802,-18.5621538371215,
6.68915892571303));
#173947=CARTESIAN_POINT('Ctrl Pts',(20.7868423666665,-18.4345722145591,
6.68146395285269));
#173948=CARTESIAN_POINT('Ctrl Pts',(20.7833021713075,-18.4207242794161,
6.68062225334265));
#173949=CARTESIAN_POINT('Ctrl Pts',(20.7774449141534,-18.3987429340034,
6.67927542418178));
#173950=CARTESIAN_POINT('Ctrl Pts',(20.7752188365562,-18.3905855751958,
6.678773237454));
#173951=CARTESIAN_POINT('Ctrl Pts',(20.7712067839709,-18.3762229493748,
6.67788475962816));
#173952=CARTESIAN_POINT('Ctrl Pts',(20.7694411667829,-18.3700120724419,
6.67749913487164));
#173953=CARTESIAN_POINT('Ctrl Pts',(20.7657306842343,-18.3571832161886,
6.67669963263889));
#173954=CARTESIAN_POINT('Ctrl Pts',(20.7637818346387,-18.3505664778366,
6.6762856289637));
#173955=CARTESIAN_POINT('Ctrl Pts',(20.7586966829697,-18.3336076187836,
6.67522024500074));
#173956=CARTESIAN_POINT('Ctrl Pts',(20.7555134890168,-18.3232798698026,
6.67456733591104));
#173957=CARTESIAN_POINT('Ctrl Pts',(20.7419000613083,-18.280284040829,6.67183173002492));
#173958=CARTESIAN_POINT('Ctrl Pts',(20.7307563860413,-18.2478489474932,
6.66972571159078));
#173959=CARTESIAN_POINT('Ctrl Pts',(20.6996742767553,-18.1640614509794,
6.66417092838132));
#173960=CARTESIAN_POINT('Ctrl Pts',(20.6785117126121,-18.1131937654685,
6.66068377289905));
#173961=CARTESIAN_POINT('Ctrl Pts',(20.6094732597096,-17.9639456559883,
6.65011410260269));
#173962=CARTESIAN_POINT('Ctrl Pts',(20.5559344158356,-17.8683935896613,
6.64288319739068));
#173963=CARTESIAN_POINT('Ctrl Pts',(20.4696791982319,-17.7390563388693,
6.63261382664497));
#173964=CARTESIAN_POINT('Ctrl Pts',(20.4428521125348,-17.7015443793991,
6.62957398240444));
#173965=CARTESIAN_POINT('Ctrl Pts',(20.4015497055692,-17.6476060843514,
6.62513733129959));
#173966=CARTESIAN_POINT('Ctrl Pts',(20.3880107982308,-17.6304804833595,
6.62371849968117));
#173967=CARTESIAN_POINT('Ctrl Pts',(20.3415181457843,-17.5735051469832,
6.61897095617013));
#173968=CARTESIAN_POINT('Ctrl Pts',(20.3073673279748,-17.5346507648916,
6.61568719385093));
#173969=CARTESIAN_POINT('Ctrl Pts',(20.2658808040086,-17.4908001476466,
6.61196388803746));
#173970=CARTESIAN_POINT('Ctrl Pts',(20.2598981389262,-17.4845536869499,
6.61143308847346));
#173971=CARTESIAN_POINT('Ctrl Pts',(20.2507671430933,-17.4751362976341,
6.6106324427902));
#173972=CARTESIAN_POINT('Ctrl Pts',(20.247646863015,-17.4719384686219,6.61036050087401));
#173973=CARTESIAN_POINT('Ctrl Pts',(20.2420201170573,-17.466208284743,6.60987312401625));
#173974=CARTESIAN_POINT('Ctrl Pts',(20.2395173736773,-17.46367237051,6.60965740621838));
#173975=CARTESIAN_POINT('Ctrl Pts',(20.2340562793087,-17.4581667666818,
6.60918901528118));
#173976=CARTESIAN_POINT('Ctrl Pts',(20.2310955165991,-17.4551995507292,
6.60893653742389));
#173977=CARTESIAN_POINT('Ctrl Pts',(20.2227310843156,-17.4468665344498,
6.60822730324664));
#173978=CARTESIAN_POINT('Ctrl Pts',(20.2173071842674,-17.4415210058994,
6.60777212076156));
#173979=CARTESIAN_POINT('Ctrl Pts',(20.1842216388275,-17.4092636006333,
6.60502312005463));
#173980=CARTESIAN_POINT('Ctrl Pts',(20.1558552863375,-17.3830811471696,
6.60278236541031));
#173981=CARTESIAN_POINT('Ctrl Pts',(20.0589373025155,-17.2984138843316,
6.59544057029809));
#173982=CARTESIAN_POINT('Ctrl Pts',(19.9873673987102,-17.2435273955039,
6.59051724223738));
#173983=CARTESIAN_POINT('Ctrl Pts',(19.7703568644642,-17.0981022828827,
6.57631246218393));
#173984=CARTESIAN_POINT('Ctrl Pts',(19.6171936690868,-17.0204373233737,
6.56709203842127));
#173985=CARTESIAN_POINT('Ctrl Pts',(19.4344700030725,-16.9541078506304,
6.55579962952865));
#173986=CARTESIAN_POINT('Ctrl Pts',(19.4124520303893,-16.9465239854499,
6.55443563902311));
#173987=CARTESIAN_POINT('Ctrl Pts',(19.3811919096339,-16.9363304601114,
6.55249269243209));
#173988=CARTESIAN_POINT('Ctrl Pts',(19.3720497605427,-16.9334179332026,
6.55192370647252));
#173989=CARTESIAN_POINT('Ctrl Pts',(19.3571822849514,-16.9287925096709,
6.55099703281094));
#173990=CARTESIAN_POINT('Ctrl Pts',(19.3514688840056,-16.9270415102135,
6.55064059927417));
#173991=CARTESIAN_POINT('Ctrl Pts',(19.339509129042,-16.9234314980434,6.54989377463234));
#173992=CARTESIAN_POINT('Ctrl Pts',(19.3332614593487,-16.9215770947044,
6.54950323717956));
#173993=CARTESIAN_POINT('Ctrl Pts',(19.3184058056801,-16.9172422493727,
6.54857362021242));
#173994=CARTESIAN_POINT('Ctrl Pts',(19.309790495537,-16.9147875538265,6.54803370769934));
#173995=CARTESIAN_POINT('Ctrl Pts',(19.2808432814633,-16.9067381316301,
6.54621680888953));
#173996=CARTESIAN_POINT('Ctrl Pts',(19.2604439218395,-16.9013926676821,
6.54493177925463));
#173997=CARTESIAN_POINT('Ctrl Pts',(19.1497950947463,-16.8741580112182,
6.53793443075258));
#173998=CARTESIAN_POINT('Ctrl Pts',(19.0582706834185,-16.8579232403246,
6.53204269793041));
#173999=CARTESIAN_POINT('Ctrl Pts',(18.8139405565176,-16.8309867181146,
6.51608860539451));
#174000=CARTESIAN_POINT('Ctrl Pts',(18.6605373395818,-16.8307533524097,
6.50581585662054));
#174001=CARTESIAN_POINT('Ctrl Pts',(18.5040735368982,-16.8475185378853,
6.4956318624244));
#174002=CARTESIAN_POINT('Ctrl Pts',(18.499695196508,-16.848001506107,6.49534715683458));
#174003=CARTESIAN_POINT('Ctrl Pts',(18.4442788129399,-16.8542895312967,
6.49174736493));
#174004=CARTESIAN_POINT('Ctrl Pts',(18.3934622119089,-16.8619371949286,
6.48848588507889));
#174005=CARTESIAN_POINT('Ctrl Pts',(18.3352295037965,-16.8728816475476,
6.48483135229389));
#174006=CARTESIAN_POINT('Ctrl Pts',(18.3274970175734,-16.874379639628,6.48434778940366));
#174007=CARTESIAN_POINT('Ctrl Pts',(18.3151814396582,-16.8768368896382,
6.48358053802955));
#174008=CARTESIAN_POINT('Ctrl Pts',(18.3105929449135,-16.8777682415491,
6.48329532655325));
#174009=CARTESIAN_POINT('Ctrl Pts',(18.3024887454088,-16.87944120792,6.48279277880801));
#174010=CARTESIAN_POINT('Ctrl Pts',(18.298971790993,-16.8801765597469,6.48257508886703));
#174011=CARTESIAN_POINT('Ctrl Pts',(18.29154023578,-16.8817501640925,6.48211595474024));
#174012=CARTESIAN_POINT('Ctrl Pts',(18.2876261427665,-16.882590565833,6.48187463516785));
#174013=CARTESIAN_POINT('Ctrl Pts',(18.2771101511795,-16.8848796964931,
6.48122756900835));
#174014=CARTESIAN_POINT('Ctrl Pts',(18.2705127033572,-16.8863489617572,
6.48082298269991));
#174015=CARTESIAN_POINT('Ctrl Pts',(18.2383282279912,-16.8936784691655,
6.47885545437729));
#174016=CARTESIAN_POINT('Ctrl Pts',(18.2128434368267,-16.8999829412734,
6.47731658043968));
#174017=CARTESIAN_POINT('Ctrl Pts',(18.1401795898599,-16.9193998116499,
6.47296659201194));
#174018=CARTESIAN_POINT('Ctrl Pts',(18.0933274841723,-16.9336775373401,
6.47020771883184));
#174019=CARTESIAN_POINT('Ctrl Pts',(17.9175621553092,-16.9939787413755,
6.45989040273254));
#174020=CARTESIAN_POINT('Ctrl Pts',(17.7927230343377,-17.0508375930593,
6.45261020107232));
#174021=CARTESIAN_POINT('Ctrl Pts',(17.5865916267845,-17.170036300437,6.43949642027855));
#174022=CARTESIAN_POINT('Ctrl Pts',(17.5027007508073,-17.2269379826017,
6.43380098422931));
#174023=CARTESIAN_POINT('Ctrl Pts',(17.4121866698885,-17.2983085155314,
6.42704597803946));
#174024=CARTESIAN_POINT('Ctrl Pts',(17.4012518620529,-17.3071083950231,
6.42621922657819));
#174025=CARTESIAN_POINT('Ctrl Pts',(17.3839289808812,-17.3213352638226,
6.424891860317));
#174026=CARTESIAN_POINT('Ctrl Pts',(17.3774841170513,-17.3266926768445,
6.42439405532392));
#174027=CARTESIAN_POINT('Ctrl Pts',(17.3661396864615,-17.3362374246486,
6.42351066773136));
#174028=CARTESIAN_POINT('Ctrl Pts',(17.3612270845954,-17.3404091528636,
6.42312572695975));
#174029=CARTESIAN_POINT('Ctrl Pts',(17.3561424637417,-17.3447670756299,
6.42272478562491));
#174030=CARTESIAN_POINT('Ctrl Pts',(17.3559513063226,-17.3449309718437,
6.42270970843043));
#174031=CARTESIAN_POINT('Ctrl Pts',(17.3556444990268,-17.3451941199501,
6.42268550358961));
#174032=CARTESIAN_POINT('Ctrl Pts',(17.355528832093,-17.3452933489667,6.42267637695556));
#174033=CARTESIAN_POINT('Ctrl Pts',(17.3553013834243,-17.3454885165824,
6.42265842756588));
#174034=CARTESIAN_POINT('Ctrl Pts',(17.355189600013,-17.3455844551966,6.42264960476726));
#174035=CARTESIAN_POINT('Ctrl Pts',(17.3549764819806,-17.3457674033349,
6.42263278143891));
#174036=CARTESIAN_POINT('Ctrl Pts',(17.354875142966,-17.3458544130278,6.42262478078877));
#174037=CARTESIAN_POINT('Ctrl Pts',(17.3546817820773,-17.3460204645072,
6.42260951307112));
#174038=CARTESIAN_POINT('Ctrl Pts',(17.3545897579858,-17.3460995052803,
6.42260224601196));
#174039=CARTESIAN_POINT('Ctrl Pts',(17.3544140446979,-17.3462504541158,
6.42258836844169));
#174040=CARTESIAN_POINT('Ctrl Pts',(17.3543303532612,-17.346322361729,6.42258175790306));
#174041=CARTESIAN_POINT('Ctrl Pts',(17.3541704369891,-17.346459783393,6.42256912522274));
#174042=CARTESIAN_POINT('Ctrl Pts',(17.3540942146795,-17.3465252933352,
6.42256310340266));
#174043=CARTESIAN_POINT('Ctrl Pts',(17.353948485064,-17.3466505599948,6.422551589135));
#174044=CARTESIAN_POINT('Ctrl Pts',(17.3538789770043,-17.3467103157724,
6.42254609672779));
#174045=CARTESIAN_POINT('Ctrl Pts',(17.3537460096147,-17.3468246422803,
6.42253558892838));
#174046=CARTESIAN_POINT('Ctrl Pts',(17.3536825496168,-17.3468792122795,
6.42253057356556));
#174047=CARTESIAN_POINT('Ctrl Pts',(17.3535610892799,-17.3469836699825,
6.42252097353842));
#174048=CARTESIAN_POINT('Ctrl Pts',(17.3535030883777,-17.3470335570941,
6.42251638889736));
#174049=CARTESIAN_POINT('Ctrl Pts',(17.3533920237486,-17.3471290952818,
6.42250760921151));
#174050=CARTESIAN_POINT('Ctrl Pts',(17.3533389595992,-17.3471747458308,
6.42250341418939));
#174051=CARTESIAN_POINT('Ctrl Pts',(17.3532373039123,-17.3472622079599,
6.42249537717822));
#174052=CARTESIAN_POINT('Ctrl Pts',(17.3531887120005,-17.3473040191231,
6.42249153520608));
#174053=CARTESIAN_POINT('Ctrl Pts',(17.3530955863933,-17.3473841568981,
6.42248417166563));
#174054=CARTESIAN_POINT('Ctrl Pts',(17.3530510524237,-17.3474224831314,
6.42248065011431));
#174055=CARTESIAN_POINT('Ctrl Pts',(17.3529656723011,-17.3474959680257,
6.42247389823852));
#174056=CARTESIAN_POINT('Ctrl Pts',(17.3529248258877,-17.3475311263988,
6.42247066792569));
#174057=CARTESIAN_POINT('Ctrl Pts',(17.3528265963618,-17.3476156835672,
6.42246289909446));
#174058=CARTESIAN_POINT('Ctrl Pts',(17.3527692145124,-17.3476650839204,
6.42245836050928));
#174059=CARTESIAN_POINT('Ctrl Pts',(17.352655536496,-17.3477629605741,6.4224493685421));
#174060=CARTESIAN_POINT('Ctrl Pts',(17.3525992344936,-17.3478114417002,
6.42244491471103));
#174061=CARTESIAN_POINT('Ctrl Pts',(17.3524876634027,-17.3479075247515,
6.42243608811409));
#174062=CARTESIAN_POINT('Ctrl Pts',(17.3524324000683,-17.3479551215323,
6.42243171581548));
#174063=CARTESIAN_POINT('Ctrl Pts',(17.3523228802671,-17.3480494577653,
6.42242305025827));
#174064=CARTESIAN_POINT('Ctrl Pts',(17.3522686236564,-17.3480961971627,
6.42241875699954));
#174065=CARTESIAN_POINT('Ctrl Pts',(17.3521610845664,-17.3481888462976,
6.42241024696516));
#174066=CARTESIAN_POINT('Ctrl Pts',(17.3521078020635,-17.3482347558857,
6.42240603019835));
#174067=CARTESIAN_POINT('Ctrl Pts',(17.3520021798921,-17.348325771863,6.42239767070273));
#174068=CARTESIAN_POINT('Ctrl Pts',(17.3519498401874,-17.3483708781218,
6.42239352798124));
#174069=CARTESIAN_POINT('Ctrl Pts',(17.3518460738484,-17.3484603126104,
6.42238531425069));
#174070=CARTESIAN_POINT('Ctrl Pts',(17.3517946470405,-17.3485046408362,
6.42238124323756));
#174071=CARTESIAN_POINT('Ctrl Pts',(17.3516926772692,-17.3485925439932,
6.42237317063892));
#174072=CARTESIAN_POINT('Ctrl Pts',(17.3516421343707,-17.3486361187222,
6.42236916906777));
#174073=CARTESIAN_POINT('Ctrl Pts',(17.3459070467533,-17.3535810029808,
6.42191508219764));
#174074=CARTESIAN_POINT('Ctrl Pts',(17.3402486644273,-17.3585124571519,
6.4214637476894));
#174075=CARTESIAN_POINT('Ctrl Pts',(17.3243532093297,-17.3725152701771,
6.42018637321097));
#174076=CARTESIAN_POINT('Ctrl Pts',(17.3141777963635,-17.3816557758,6.41935744412653));
#174077=CARTESIAN_POINT('Ctrl Pts',(17.2915006215952,-17.4024271254078,
6.41748432679498));
#174078=CARTESIAN_POINT('Ctrl Pts',(17.2790496789871,-17.4141118093299,
6.41643788148387));
#174079=CARTESIAN_POINT('Ctrl Pts',(17.2402933392558,-17.4513749364202,
6.41312271720485));
#174080=CARTESIAN_POINT('Ctrl Pts',(17.2145118654067,-17.4774862759698,
6.41083142260862));
#174081=CARTESIAN_POINT('Ctrl Pts',(17.1336459612229,-17.5637607586575,
6.40335973354851));
#174082=CARTESIAN_POINT('Ctrl Pts',(17.0813595156129,-17.6264365499411,
6.39807659050608));
#174083=CARTESIAN_POINT('Ctrl Pts',(17.00200945163,-17.7335674757035,6.38932606776703));
#174084=CARTESIAN_POINT('Ctrl Pts',(16.9727332252932,-17.7762839414903,
6.38590397144071));
#174085=CARTESIAN_POINT('Ctrl Pts',(16.878437326321,-17.9253076325162,6.37425085273708));
#174086=CARTESIAN_POINT('Ctrl Pts',(16.8212373151914,-18.0362729447741,
6.36603542867206));
#174087=CARTESIAN_POINT('Ctrl Pts',(16.7705660899994,-18.1603530211319,
6.35775868565974));
#174088=CARTESIAN_POINT('Ctrl Pts',(16.7670644075452,-18.1690938493287,
6.35718035341813));
#174089=CARTESIAN_POINT('Ctrl Pts',(16.761951806765,-18.1821066556356,6.35632667497136));
#174090=CARTESIAN_POINT('Ctrl Pts',(16.7602962549954,-18.186360812135,6.35604874332209));
#174091=CARTESIAN_POINT('Ctrl Pts',(16.757370392281,-18.193951755447,6.35555490977215));
#174092=CARTESIAN_POINT('Ctrl Pts',(16.7560947526008,-18.197286425101,6.35533869165968));
#174093=CARTESIAN_POINT('Ctrl Pts',(16.7533649789617,-18.2044768272441,
6.35487402918853));
#174094=CARTESIAN_POINT('Ctrl Pts',(16.7519136689214,-18.2083335712921,
6.35462575431155));
#174095=CARTESIAN_POINT('Ctrl Pts',(16.7487731480944,-18.2167537661666,
6.35408574701506));
#174096=CARTESIAN_POINT('Ctrl Pts',(16.7470883891837,-18.2213188591448,
6.35379427708308));
#174097=CARTESIAN_POINT('Ctrl Pts',(16.7454193692319,-18.2258897639243,
6.3535036965741));
#174098=CARTESIAN_POINT('',(16.6170007251258,-18.9537521935254,6.8890562790225));
#174099=CARTESIAN_POINT('Ctrl Pts',(16.6170007251258,-18.9537521935254,
6.8890562790225));
#174100=CARTESIAN_POINT('Ctrl Pts',(16.6170993834536,-19.0729511321297,
6.88186870628082));
#174101=CARTESIAN_POINT('Ctrl Pts',(16.6272689227094,-19.1917453566806,
6.87468113353914));
#174102=CARTESIAN_POINT('Ctrl Pts',(16.6472858251195,-19.3088094062,6.86749356079746));
#174103=CARTESIAN_POINT('Ctrl Pts',(16.6595066892529,-19.3802801969733,
6.86310535186656));
#174104=CARTESIAN_POINT('Ctrl Pts',(16.6754275106646,-19.4512619171913,
6.85871714293566));
#174105=CARTESIAN_POINT('Ctrl Pts',(16.6949957094314,-19.5213421669286,
6.85432893400477));
#174106=CARTESIAN_POINT('Ctrl Pts',(16.7145348657469,-19.5913184059559,
6.8499472379035));
#174107=CARTESIAN_POINT('Ctrl Pts',(16.7377105245955,-19.6603953697142,
6.84556554180223));
#174108=CARTESIAN_POINT('Ctrl Pts',(16.7644188550042,-19.7281695132361,
6.84118384570096));
#174109=CARTESIAN_POINT('Ctrl Pts',(16.7910958009992,-19.7958640167457,
6.83680729844132));
#174110=CARTESIAN_POINT('Ctrl Pts',(16.8212969962484,-19.8622582946367,
6.83243075118168));
#174111=CARTESIAN_POINT('Ctrl Pts',(16.8548689277714,-19.9269643139033,
6.82805420392204));
#174112=CARTESIAN_POINT('Ctrl Pts',(16.8884195684633,-19.9916292975528,
6.82368043220506));
#174113=CARTESIAN_POINT('Ctrl Pts',(16.9253364824028,-20.0546077198004,
6.81930666048808));
#174114=CARTESIAN_POINT('Ctrl Pts',(16.9654187837192,-20.1155331887913,
6.81493288877111));
#174115=CARTESIAN_POINT('Ctrl Pts',(17.0054888878568,-20.1764401179574,
6.81056044800755));
#174116=CARTESIAN_POINT('Ctrl Pts',(17.0487222020848,-20.2352949313846,
6.806188007244));
#174117=CARTESIAN_POINT('Ctrl Pts',(17.0948736736053,-20.2917588910397,
6.80181556648045));
#174118=CARTESIAN_POINT('Ctrl Pts',(17.1410263252241,-20.3482242944845,
6.7974430139131));
#174119=CARTESIAN_POINT('Ctrl Pts',(17.1900969754572,-20.4022983505563,
6.79307046134575));
#174120=CARTESIAN_POINT('Ctrl Pts',(17.2418003884899,-20.4536755040318,
6.78869790877841));
#174121=CARTESIAN_POINT('Ctrl Pts',(17.2935574612748,-20.5051059786551,
6.78432081821108));
#174122=CARTESIAN_POINT('Ctrl Pts',(17.3479524093387,-20.5538336216567,
6.77994372764375));
#174123=CARTESIAN_POINT('Ctrl Pts',(17.4046638348791,-20.5995904709914,
6.77556663707642));
#174124=CARTESIAN_POINT('Ctrl Pts',(17.4614062326338,-20.6453723098397,
6.77118715601747));
#174125=CARTESIAN_POINT('Ctrl Pts',(17.5204672358496,-20.6881798414323,
6.76680767495852));
#174126=CARTESIAN_POINT('Ctrl Pts',(17.5814953303094,-20.7277877086919,
6.76242819389958));
#174127=CARTESIAN_POINT('Ctrl Pts',(17.6426315966569,-20.7674657806304,
6.75804095023986));
#174128=CARTESIAN_POINT('Ctrl Pts',(17.7057414989265,-20.8039326211616,
6.75365370658013));
#174129=CARTESIAN_POINT('Ctrl Pts',(17.7704482580137,-20.8370084987912,
6.74926646292041));
#174130=CARTESIAN_POINT('Ctrl Pts',(17.8144426190642,-20.8594969083952,
6.74628355998562));
#174131=CARTESIAN_POINT('Ctrl Pts',(17.8591746727794,-20.8804187619501,
6.74330065705082));
#174132=CARTESIAN_POINT('Ctrl Pts',(17.9045214391031,-20.8997305555473,
6.74031775411602));
#174133=CARTESIAN_POINT('Ctrl Pts',(17.9712319856139,-20.9281405262995,
6.73592954518513));
#174134=CARTESIAN_POINT('Ctrl Pts',(18.0395340178843,-20.9531746938961,
6.73154133625423));
#174135=CARTESIAN_POINT('Ctrl Pts',(18.1090523123257,-20.9746540454735,
6.72715312732333));
#174136=CARTESIAN_POINT('Ctrl Pts',(18.1784674300917,-20.9961015181319,
6.72277143122207));
#174137=CARTESIAN_POINT('Ctrl Pts',(18.2490947695194,-21.0140045070018,
6.71838973512081));
#174138=CARTESIAN_POINT('Ctrl Pts',(18.3205388114172,-21.0282318862631,
6.71400803901954));
#174139=CARTESIAN_POINT('Ctrl Pts',(18.39189890088,-21.0424425472215,6.70963149175991));
#174140=CARTESIAN_POINT('Ctrl Pts',(18.4640733156415,-21.0529860848151,
6.70525494450027));
#174141=CARTESIAN_POINT('Ctrl Pts',(18.5366526876864,-21.0597815442599,
6.70087839724063));
#174142=CARTESIAN_POINT('Ctrl Pts',(18.6091860309483,-21.066572694123,6.69650462552366));
#174143=CARTESIAN_POINT('Ctrl Pts',(18.6821233428378,-21.0696204372107,
6.69213085380669));
#174144=CARTESIAN_POINT('Ctrl Pts',(18.7550478100763,-21.0688953657871,
6.68775708208972));
#174145=CARTESIAN_POINT('Ctrl Pts',(18.8279500861544,-21.0681705150053,
6.68338464132617));
#174146=CARTESIAN_POINT('Ctrl Pts',(18.9008390432775,-21.0636751337982,
6.67901220056262));
#174147=CARTESIAN_POINT('Ctrl Pts',(18.9732972139342,-21.0554319203158,
6.67463975979907));
#174148=CARTESIAN_POINT('Ctrl Pts',(19.0457572373544,-21.0471884960535,
6.67026720723173));
#174149=CARTESIAN_POINT('Ctrl Pts',(19.1177859733785,-21.0351971057623,
6.66589465466438));
#174150=CARTESIAN_POINT('Ctrl Pts',(19.1889721056824,-21.0195321963759,
6.66152210209704));
#174151=CARTESIAN_POINT('Ctrl Pts',(19.2602321176395,-21.0038510293557,
6.65714501152972));
#174152=CARTESIAN_POINT('Ctrl Pts',(19.3306473077923,-20.9844888351851,
6.65276792096239));
#174153=CARTESIAN_POINT('Ctrl Pts',(19.399818395932,-20.9615708157809,6.64839083039507));
#174154=CARTESIAN_POINT('Ctrl Pts',(19.4690272609703,-20.9386402799958,
6.64401134933613));
#174155=CARTESIAN_POINT('Ctrl Pts',(19.5369902214611,-20.9121502278397,
6.63963186827719));
#174156=CARTESIAN_POINT('Ctrl Pts',(19.6033275197872,-20.8822742456295,
6.63525238721825));
#174157=CARTESIAN_POINT('Ctrl Pts',(19.6697824005294,-20.8523453084414,
6.63086514355853));
#174158=CARTESIAN_POINT('Ctrl Pts',(19.734605435538,-20.8190186771225,6.62647789989881));
#174159=CARTESIAN_POINT('Ctrl Pts',(19.7974415556865,-20.7825138780242,
6.62209065623909));
#174160=CARTESIAN_POINT('Ctrl Pts',(19.8401640625136,-20.7576941322312,
6.61910775330426));
#174161=CARTESIAN_POINT('Ctrl Pts',(19.8819686426644,-20.7314061565723,
6.61612485036943));
#174162=CARTESIAN_POINT('Ctrl Pts',(19.922752149464,-20.7037298099721,6.61314194743459));
#174163=CARTESIAN_POINT('Ctrl Pts',(19.982749592452,-20.6630145758598,6.6087537385037));
#174164=CARTESIAN_POINT('Ctrl Pts',(20.0407699602754,-20.6191338958608,
6.6043655295728));
#174165=CARTESIAN_POINT('Ctrl Pts',(20.0964596300333,-20.572306377365,6.5999773206419));
#174166=CARTESIAN_POINT('Ctrl Pts',(20.1520666470878,-20.5255483586707,
6.59559562454063));
#174167=CARTESIAN_POINT('Ctrl Pts',(20.2053494667968,-20.475852491549,6.59121392843937));
#174168=CARTESIAN_POINT('Ctrl Pts',(20.2559837460598,-20.4234803691282,
6.5868322323381));
#174169=CARTESIAN_POINT('Ctrl Pts',(20.3065585260151,-20.3711697881192,
6.58245568507846));
#174170=CARTESIAN_POINT('Ctrl Pts',(20.3544906143947,-20.3161895440789,
6.57807913781882));
#174171=CARTESIAN_POINT('Ctrl Pts',(20.3994903578942,-20.2588400314351,
6.57370259055918));
#174172=CARTESIAN_POINT('Ctrl Pts',(20.4444615632104,-20.2015268890188,
6.5693288188422));
#174173=CARTESIAN_POINT('Ctrl Pts',(20.4865038163916,-20.1418478378278,
6.56495504712523));
#174174=CARTESIAN_POINT('Ctrl Pts',(20.5253667770637,-20.0801374340179,
6.56058127540825));
#174175=CARTESIAN_POINT('Ctrl Pts',(20.5642179116064,-20.0184458088911,
6.5562088346447));
#174176=CARTESIAN_POINT('Ctrl Pts',(20.599891417463,-19.9547244662924,6.55183639388115));
#174177=CARTESIAN_POINT('Ctrl Pts',(20.6321804129397,-19.889336716411,6.54746395311759));
#174178=CARTESIAN_POINT('Ctrl Pts',(20.6644702340495,-19.8239472945576,
6.54309140055025));
#174179=CARTESIAN_POINT('Ctrl Pts',(20.6933751611701,-19.756891814226,6.5387188479829));
#174180=CARTESIAN_POINT('Ctrl Pts',(20.7187351546661,-19.6885564240657,
6.53434629541556));
#174181=CARTESIAN_POINT('Ctrl Pts',(20.7441214677199,-19.62015011286,6.52996920484823));
#174182=CARTESIAN_POINT('Ctrl Pts',(20.7659553334561,-19.5504616929154,
6.5255921142809));
#174183=CARTESIAN_POINT('Ctrl Pts',(20.784125904069,-19.479894665123,6.52121502371357));
#174184=CARTESIAN_POINT('Ctrl Pts',(20.8023063983049,-19.4092890980576,
6.51683554265463));
#174185=CARTESIAN_POINT('Ctrl Pts',(20.8168195180774,-19.337804440848,6.51245606159569));
#174186=CARTESIAN_POINT('Ctrl Pts',(20.8276056664129,-19.2658539685332,
6.50807658053674));
#174187=CARTESIAN_POINT('Ctrl Pts',(20.8384109331238,-19.1937759644891,
6.50368933687702));
#174188=CARTESIAN_POINT('Ctrl Pts',(20.8454759896224,-19.1212309770712,
6.4993020932173));
#174189=CARTESIAN_POINT('Ctrl Pts',(20.8487932306455,-19.0486363886742,
6.49491484955758));
#174190=CARTESIAN_POINT('Ctrl Pts',(20.8510486348926,-18.9992790637622,
6.49193194662277));
#174191=CARTESIAN_POINT('Ctrl Pts',(20.8515726338748,-18.9498988449408,
6.48894904368796));
#174192=CARTESIAN_POINT('Ctrl Pts',(20.8503765449711,-18.9006256883613,
6.48596614075315));
#174193=CARTESIAN_POINT('Ctrl Pts',(20.8486169543561,-18.8281389496101,
6.48157793182225));
#174194=CARTESIAN_POINT('Ctrl Pts',(20.8431255714046,-18.7556012223724,
6.47718972289135));
#174195=CARTESIAN_POINT('Ctrl Pts',(20.8338948009668,-18.6834281755797,
6.47280151396046));
#174196=CARTESIAN_POINT('Ctrl Pts',(20.8246777305229,-18.6113622455548,
6.46841981785919));
#174197=CARTESIAN_POINT('Ctrl Pts',(20.811732350535,-18.5396603960523,6.46403812175792));
#174198=CARTESIAN_POINT('Ctrl Pts',(20.7951030586572,-18.46873694369,6.45965642565666));
#174199=CARTESIAN_POINT('Ctrl Pts',(20.7784933075207,-18.3978968320285,
6.45527987839702));
#174200=CARTESIAN_POINT('Ctrl Pts',(20.758208353431,-18.3278337678025,6.45090333113738));
#174201=CARTESIAN_POINT('Ctrl Pts',(20.7343439967234,-18.2589539014087,
6.44652678387774));
#174202=CARTESIAN_POINT('Ctrl Pts',(20.710494774444,-18.1901177176251,6.44215301216076));
#174203=CARTESIAN_POINT('Ctrl Pts',(20.6830708110596,-18.1224636975236,
6.43777924044379));
#174204=CARTESIAN_POINT('Ctrl Pts',(20.652217910856,-18.0563834266433,6.43340546872682));
#174205=CARTESIAN_POINT('Ctrl Pts',(20.6213743992936,-17.9903232642113,
6.42903302796327));
#174206=CARTESIAN_POINT('Ctrl Pts',(20.5871042264079,-17.9258363370628,
6.42466058719971));
#174207=CARTESIAN_POINT('Ctrl Pts',(20.5496008974357,-17.8632932528772,
6.42028814643616));
#174208=CARTESIAN_POINT('Ctrl Pts',(20.5120966094992,-17.800748569458,6.41591559386882));
#174209=CARTESIAN_POINT('Ctrl Pts',(20.4713592511252,-17.7401482403578,
6.41154304130147));
#174210=CARTESIAN_POINT('Ctrl Pts',(20.4276268857995,-17.681835848523,6.40717048873413));
#174211=CARTESIAN_POINT('Ctrl Pts',(20.3838491333754,-17.6234629378886,
6.4027933981668));
#174212=CARTESIAN_POINT('Ctrl Pts',(20.3370704580446,-17.567383092118,6.39841630759947));
#174213=CARTESIAN_POINT('Ctrl Pts',(20.2875701403861,-17.5139079240533,
6.39403921703215));
#174214=CARTESIAN_POINT('Ctrl Pts',(20.2380427887669,-17.4604035512145,
6.38965973597321));
#174215=CARTESIAN_POINT('Ctrl Pts',(20.1857911812157,-17.409507025103,6.38528025491427));
#174216=CARTESIAN_POINT('Ctrl Pts',(20.1311305579265,-17.3614921552825,
6.38090077385533));
#174217=CARTESIAN_POINT('Ctrl Pts',(20.0763730490495,-17.3133921794275,
6.37651353019561));
#174218=CARTESIAN_POINT('Ctrl Pts',(20.0191983762075,-17.2681843592168,
6.37212628653589));
#174219=CARTESIAN_POINT('Ctrl Pts',(19.9599533753576,-17.2261010106471,
6.36773904287617));
#174220=CARTESIAN_POINT('Ctrl Pts',(19.9196724836144,-17.1974883887616,
6.36475613994135));
#174221=CARTESIAN_POINT('Ctrl Pts',(19.8784351648852,-17.170319212664,6.36177323700653));
#174222=CARTESIAN_POINT('Ctrl Pts',(19.8363568176099,-17.1446543090297,
6.35879033407171));
#174223=CARTESIAN_POINT('Ctrl Pts',(19.7744545085686,-17.1068981494093,
6.35440212514082));
#174224=CARTESIAN_POINT('Ctrl Pts',(19.7104893778666,-17.0722522374744,
6.35001391620992));
#174225=CARTESIAN_POINT('Ctrl Pts',(19.6448068261837,-17.0409479532526,
6.34562570727902));
#174226=CARTESIAN_POINT('Ctrl Pts',(19.5792217582977,-17.009690129779,6.34124401117776));
#174227=CARTESIAN_POINT('Ctrl Pts',(19.5119247612709,-16.9817642944955,
6.33686231507649));
#174228=CARTESIAN_POINT('Ctrl Pts',(19.4432882414199,-16.9573573777282,
6.33248061897523));
#174229=CARTESIAN_POINT('Ctrl Pts',(19.374732374942,-16.9329791410304,6.32810407171559));
#174230=CARTESIAN_POINT('Ctrl Pts',(19.3048405647341,-16.9121117694419,
6.32372752445595));
#174231=CARTESIAN_POINT('Ctrl Pts',(19.2340061739096,-16.8948945515477,
6.31935097719632));
#174232=CARTESIAN_POINT('Ctrl Pts',(19.1632167052263,-16.8776882525628,
6.31497720547934));
#174233=CARTESIAN_POINT('Ctrl Pts',(19.0914863095583,-16.8641276279119,
6.31060343376237));
#174234=CARTESIAN_POINT('Ctrl Pts',(19.019223169469,-16.8543020370897,6.3062296620454));
#174235=CARTESIAN_POINT('Ctrl Pts',(18.9469820192958,-16.8444794362278,
6.30185722128185));
#174236=CARTESIAN_POINT('Ctrl Pts',(18.8742089242435,-16.838389677678,6.2974847805183));
#174237=CARTESIAN_POINT('Ctrl Pts',(18.8013202474354,-16.8360706570669,
6.29311233975475));
#174238=CARTESIAN_POINT('Ctrl Pts',(18.7284297068557,-16.8337515771582,
6.2887397871874));
#174239=CARTESIAN_POINT('Ctrl Pts',(18.6554240608497,-16.8352034399581,
6.28436723462006));
#174240=CARTESIAN_POINT('Ctrl Pts',(18.5827210675518,-16.8404120466821,
6.27999468205272));
#174241=CARTESIAN_POINT('Ctrl Pts',(18.5099426203453,-16.8456260590946,
6.27561759148539));
#174242=CARTESIAN_POINT('Ctrl Pts',(18.4374679351514,-16.8546045652847,
6.27124050091807));
#174243=CARTESIAN_POINT('Ctrl Pts',(18.365710198337,-16.8672814046037,6.26686341035074));
#174244=CARTESIAN_POINT('Ctrl Pts',(18.2939132719592,-16.8799651672152,
6.2624839292918));
#174245=CARTESIAN_POINT('Ctrl Pts',(18.222834543912,-16.8963511759144,6.25810444823286));
#174246=CARTESIAN_POINT('Ctrl Pts',(18.1528748782451,-16.9163225715096,
6.25372496717392));
#174247=CARTESIAN_POINT('Ctrl Pts',(18.0827912095404,-16.9363293662694,
6.2493377235142));
#174248=CARTESIAN_POINT('Ctrl Pts',(18.0138310210299,-16.9599340823954,
6.24495047985448));
#174249=CARTESIAN_POINT('Ctrl Pts',(17.9463773894275,-16.9869708339786,
6.24056323619476));
#174250=CARTESIAN_POINT('Ctrl Pts',(17.9005154197541,-17.0053532198,6.23758033325993));
#174251=CARTESIAN_POINT('Ctrl Pts',(17.8553494637707,-17.0253211191867,
6.23459743032511));
#174252=CARTESIAN_POINT('Ctrl Pts',(17.810993130072,-17.0468104246386,6.23161452739028));
#174253=CARTESIAN_POINT('Ctrl Pts',(17.7457580547156,-17.0784148505146,
6.22722755755964));
#174254=CARTESIAN_POINT('Ctrl Pts',(17.6820207921123,-17.1134353687213,
6.22284058772901));
#174255=CARTESIAN_POINT('Ctrl Pts',(17.6201625345959,-17.1517069403394,
6.21845361789837));
#174256=CARTESIAN_POINT('Ctrl Pts',(17.5583882674463,-17.1899265472972,
6.21407260464039));
#174257=CARTESIAN_POINT('Ctrl Pts',(17.4984883504377,-17.231388199258,6.20969159138242));
#174258=CARTESIAN_POINT('Ctrl Pts',(17.4408213800094,-17.2758800589459,
6.20531057812444));
#174259=CARTESIAN_POINT('Ctrl Pts',(17.3832136794369,-17.3203261900983,
6.20093406765239));
#174260=CARTESIAN_POINT('Ctrl Pts',(17.3278347507031,-17.3677960551435,
6.19655755718035));
#174261=CARTESIAN_POINT('Ctrl Pts',(17.2750146386688,-17.4180343173913,
6.19218104670831));
#174262=CARTESIAN_POINT('Ctrl Pts',(17.2222313878218,-17.4682375202285,
6.1878075904398));
#174263=CARTESIAN_POINT('Ctrl Pts',(17.1720037564618,-17.5212049524845,
6.18343413417128));
#174264=CARTESIAN_POINT('Ctrl Pts',(17.1246277766843,-17.5766418478011,
6.17906067790277));
#174265=CARTESIAN_POINT('Ctrl Pts',(17.0772569743065,-17.6320726847952,
6.17468769957965));
#174266=CARTESIAN_POINT('Ctrl Pts',(17.0327375273207,-17.6899720904902,
6.17031472125653));
#174267=CARTESIAN_POINT('Ctrl Pts',(16.9913267830639,-17.7500103748477,
6.16594174293342));
#174268=CARTESIAN_POINT('Ctrl Pts',(16.9499189762258,-17.8100444004656,
6.16156907480197));
#174269=CARTESIAN_POINT('Ctrl Pts',(16.9116197015766,-17.8722166017246,
6.15719640667052));
#174270=CARTESIAN_POINT('Ctrl Pts',(16.8766431790062,-17.9361680062591,
6.15282373853907));
#174271=CARTESIAN_POINT('Ctrl Pts',(16.8416426205708,-18.0001633581963,
6.14844806551025));
#174272=CARTESIAN_POINT('Ctrl Pts',(16.8099695961693,-18.0659399263405,
6.14407239248142));
#174273=CARTESIAN_POINT('Ctrl Pts',(16.7817919876685,-18.1331148575113,
6.1396967194526));
#174274=CARTESIAN_POINT('Ctrl Pts',(16.768936728617,-18.1637615726841,6.1377004389553));
#174275=CARTESIAN_POINT('Ctrl Pts',(16.7568083399034,-18.194699064005,6.13570415845801));
#174276=CARTESIAN_POINT('Ctrl Pts',(16.7454193692319,-18.2258897639242,
6.13370787796071));
#174277=CARTESIAN_POINT('Ctrl Pts',(16.7486737197731,-18.2270709325543,
6.93361858681016));
#174278=CARTESIAN_POINT('Ctrl Pts',(16.6638908378346,-18.4600474814419,
6.9187647400854));
#174279=CARTESIAN_POINT('Ctrl Pts',(16.617844373311,-18.7072442534351,6.90391089336065));
#174280=CARTESIAN_POINT('Ctrl Pts',(16.6156461116265,-18.9537405764282,
6.88905704663589));
#174281=CARTESIAN_POINT('Origin',(18.734,-18.952,0.));
#174282=CARTESIAN_POINT('',(16.7454193380512,-18.2258898493182,7.95734463868439));
#174283=CARTESIAN_POINT('',(16.7454193803187,-18.2258897335611,7.73405220804246));
#174284=CARTESIAN_POINT('',(16.7454193692319,-18.2258897639242,0.));
#174285=CARTESIAN_POINT('',(16.6170007998212,-18.953910682177,7.9107295246413));
#174286=CARTESIAN_POINT('Ctrl Pts',(16.7454193380512,-18.2258898493182,
7.95734463868439));
#174287=CARTESIAN_POINT('Ctrl Pts',(16.7388878433806,-18.243777498986,7.9562441231521));
#174288=CARTESIAN_POINT('Ctrl Pts',(16.7325959958868,-18.2617579488697,
7.95513588188335));
#174289=CARTESIAN_POINT('Ctrl Pts',(16.7220479742774,-18.2932597408547,
7.95318937778389));
#174290=CARTESIAN_POINT('Ctrl Pts',(16.7176850471954,-18.3067375112457,
7.95235505144709));
#174291=CARTESIAN_POINT('Ctrl Pts',(16.7109455013963,-18.3282930398624,
7.95101781937374));
#174292=CARTESIAN_POINT('Ctrl Pts',(16.708481192049,-18.3363430890846,7.95051779053978));
#174293=CARTESIAN_POINT('Ctrl Pts',(16.7042135147882,-18.350587130326,7.94963182308968));
#174294=CARTESIAN_POINT('Ctrl Pts',(16.7023903094468,-18.3567751020104,
7.94924653872907));
#174295=CARTESIAN_POINT('Ctrl Pts',(16.698671982321,-18.3696112555395,7.94844645204706));
#174296=CARTESIAN_POINT('Ctrl Pts',(16.696781087097,-18.3762605725066,7.94803151715826));
#174297=CARTESIAN_POINT('Ctrl Pts',(16.6919991061119,-18.3933949133956,
7.94696100415976));
#174298=CARTESIAN_POINT('Ctrl Pts',(16.6891562199663,-18.4038930745159,
7.94630386874284));
#174299=CARTESIAN_POINT('Ctrl Pts',(16.6831809228324,-18.4266522578334,
7.94487642810954));
#174300=CARTESIAN_POINT('Ctrl Pts',(16.6800773158945,-18.4389203431502,
7.94410521854318));
#174301=CARTESIAN_POINT('Ctrl Pts',(16.6713662558257,-18.4747000300723,
7.94185062425237));
#174302=CARTESIAN_POINT('Ctrl Pts',(16.6660513913002,-18.4982801519989,
7.94035801902177));
#174303=CARTESIAN_POINT('Ctrl Pts',(16.6316558078731,-18.6640664717024,
7.92981461318329));
#174304=CARTESIAN_POINT('Ctrl Pts',(16.6168699505192,-18.8088166883431,
7.92031687728472));
#174305=CARTESIAN_POINT('Ctrl Pts',(16.6170008616855,-18.9539100721132,
7.91072945673524));
#174306=CARTESIAN_POINT('Ctrl Pts',(16.6170008622295,-18.9539106750009,
7.91072941689788));
#174307=CARTESIAN_POINT('Ctrl Pts',(16.6171115217675,-19.076519777243,7.90262770333203));
#174308=CARTESIAN_POINT('Ctrl Pts',(16.6278735763027,-19.1989019504627,
7.89450601028431));
#174309=CARTESIAN_POINT('Ctrl Pts',(16.651355511568,-19.3320510967405,7.88604139066189));
#174310=CARTESIAN_POINT('Ctrl Pts',(16.653648122358,-19.3444066550615,7.88525964948426));
#174311=CARTESIAN_POINT('Ctrl Pts',(16.6573287548186,-19.3633030864107,
7.88407054302234));
#174312=CARTESIAN_POINT('Ctrl Pts',(16.6586379310683,-19.3698587978723,
7.88365920698068));
#174313=CARTESIAN_POINT('Ctrl Pts',(16.6608486751434,-19.3806623838382,
7.88298344279256));
#174314=CARTESIAN_POINT('Ctrl Pts',(16.6617322871274,-19.3849138274746,
7.88271805353515));
#174315=CARTESIAN_POINT('Ctrl Pts',(16.6634789752581,-19.3931900145513,
7.88220251642844));
#174316=CARTESIAN_POINT('Ctrl Pts',(16.66434072061,-19.3972150163006,7.88195229568187));
#174317=CARTESIAN_POINT('Ctrl Pts',(16.6659719860138,-19.4047271642203,
7.88148626424512));
#174318=CARTESIAN_POINT('Ctrl Pts',(16.6667385814108,-19.4082148389771,
7.88127029567999));
#174319=CARTESIAN_POINT('Ctrl Pts',(16.6685067296305,-19.4161631714684,
7.88077899629613));
#174320=CARTESIAN_POINT('Ctrl Pts',(16.6695139068702,-19.4206225259872,
7.88050399138715));
#174321=CARTESIAN_POINT('Ctrl Pts',(16.6726472979753,-19.434289685709,7.87966300011892));
#174322=CARTESIAN_POINT('Ctrl Pts',(16.6748207597528,-19.4434866906781,
7.87909965574805));
#174323=CARTESIAN_POINT('Ctrl Pts',(16.7060513529335,-19.5717941851,7.87127264400984));
#174324=CARTESIAN_POINT('Ctrl Pts',(16.7453452201725,-19.6881939778768,
7.86455350603832));
#174325=CARTESIAN_POINT('Ctrl Pts',(16.8230773612645,-19.8658632020382,
7.85400319292143));
#174326=CARTESIAN_POINT('Ctrl Pts',(16.8549331345859,-19.9296905752479,
7.85014915513843));
#174327=CARTESIAN_POINT('Ctrl Pts',(16.9337301852796,-20.06943621804,7.84135924496039));
#174328=CARTESIAN_POINT('Ctrl Pts',(16.9823692282751,-20.1442342433673,
7.83640088446753));
#174329=CARTESIAN_POINT('Ctrl Pts',(17.0559431208771,-20.243115176939,7.8293099492823));
#174330=CARTESIAN_POINT('Ctrl Pts',(17.0769699627459,-20.2699926221172,
7.82732374507707));
#174331=CARTESIAN_POINT('Ctrl Pts',(17.1055477671658,-20.3047567339904,
7.82466995656501));
#174332=CARTESIAN_POINT('Ctrl Pts',(17.1125238594664,-20.3131107871754,
7.82402557515981));
#174333=CARTESIAN_POINT('Ctrl Pts',(17.1240367787783,-20.3266836866202,
7.82296750386227));
#174334=CARTESIAN_POINT('Ctrl Pts',(17.1285353613239,-20.3319348188096,
7.82255538620189));
#174335=CARTESIAN_POINT('Ctrl Pts',(17.1372800548251,-20.3420417345859,
7.82175675862704));
#174336=CARTESIAN_POINT('Ctrl Pts',(17.1415227966835,-20.3469003414935,
7.82137039098903));
#174337=CARTESIAN_POINT('Ctrl Pts',(17.1513514831502,-20.3580524465649,
7.82047783722391));
#174338=CARTESIAN_POINT('Ctrl Pts',(17.1569528523282,-20.3643321497455,
7.81997100799802));
#174339=CARTESIAN_POINT('Ctrl Pts',(17.1720750619579,-20.3810835485491,
7.81860750014261));
#174340=CARTESIAN_POINT('Ctrl Pts',(17.1816635957588,-20.3914933044688,
7.8177479646193));
#174341=CARTESIAN_POINT('Ctrl Pts',(17.265823056454,-20.4810419237264,7.81024568946596));
#174342=CARTESIAN_POINT('Ctrl Pts',(17.3462728239971,-20.5544105810415,
7.80334335793242));
#174343=CARTESIAN_POINT('Ctrl Pts',(17.5090247580217,-20.6813552124303,
7.7899035908775));
#174344=CARTESIAN_POINT('Ctrl Pts',(17.5901246453396,-20.7360351827152,
7.78341836997606));
#174345=CARTESIAN_POINT('Ctrl Pts',(17.7369467988554,-20.8208878484442,
7.77224124367338));
#174346=CARTESIAN_POINT('Ctrl Pts',(17.8009843717867,-20.8536677278415,
7.76753719849889));
#174347=CARTESIAN_POINT('Ctrl Pts',(17.8972767156947,-20.8969206459371,
7.76082211149693));
#174348=CARTESIAN_POINT('Ctrl Pts',(17.9283104656962,-20.9099802971092,
7.75871046801823));
#174349=CARTESIAN_POINT('Ctrl Pts',(17.9664249726907,-20.924959871533,7.75619159313983));
#174350=CARTESIAN_POINT('Ctrl Pts',(17.9732193413863,-20.9275897525189,
7.75574541884126));
#174351=CARTESIAN_POINT('Ctrl Pts',(17.9839074333896,-20.9316634523034,
7.755048162355));
#174352=CARTESIAN_POINT('Ctrl Pts',(17.987791984554,-20.9331309500479,7.75479569918502));
#174353=CARTESIAN_POINT('Ctrl Pts',(17.9950209767194,-20.9358376252837,
7.75432767776961));
#174354=CARTESIAN_POINT('Ctrl Pts',(17.9983641988263,-20.9370797688359,
7.75411194825751));
#174355=CARTESIAN_POINT('Ctrl Pts',(18.0059513417284,-20.9398769024159,
7.75362398255835));
#174356=CARTESIAN_POINT('Ctrl Pts',(18.0101971021762,-20.9414267500821,
7.75335205481275));
#174357=CARTESIAN_POINT('Ctrl Pts',(18.0228091197682,-20.9459848480949,
7.75254757455099));
#174358=CARTESIAN_POINT('Ctrl Pts',(18.0311895194472,-20.948954049858,7.75201728824248));
#174359=CARTESIAN_POINT('Ctrl Pts',(18.0942291797181,-20.9708431992103,
7.74805857365614));
#174360=CARTESIAN_POINT('Ctrl Pts',(18.1496297674981,-20.9875705011626,
7.74474953633496));
#174361=CARTESIAN_POINT('Ctrl Pts',(18.3636968877658,-21.0427420527988,
7.73236241282067));
#174362=CARTESIAN_POINT('Ctrl Pts',(18.5259285032051,-21.0650639754516,
7.72375592421126));
#174363=CARTESIAN_POINT('Ctrl Pts',(18.7491574877104,-21.0697972336905,
7.71138810956231));
#174364=CARTESIAN_POINT('Ctrl Pts',(18.8092159985676,-21.0685152079866,
7.70801427462215));
#174365=CARTESIAN_POINT('Ctrl Pts',(18.8932732959909,-21.0631385600472,
7.70317746656741));
#174366=CARTESIAN_POINT('Ctrl Pts',(18.9173818273774,-21.0611811303556,
7.70177705748212));
#174367=CARTESIAN_POINT('Ctrl Pts',(18.9594296016217,-21.0570408223668,
7.69930862404411));
#174368=CARTESIAN_POINT('Ctrl Pts',(18.9773845148172,-21.0550404934509,
7.69824627062485));
#174369=CARTESIAN_POINT('Ctrl Pts',(19.0037818369706,-21.051757038755,7.69667131928106));
#174370=CARTESIAN_POINT('Ctrl Pts',(19.0122459006903,-21.0506522048338,
7.6961643408173));
#174371=CARTESIAN_POINT('Ctrl Pts',(19.027090020576,-21.0486231889878,7.69527163609937));
#174372=CARTESIAN_POINT('Ctrl Pts',(19.0334730069536,-21.0477209913177,
7.69488660955054));
#174373=CARTESIAN_POINT('Ctrl Pts',(19.0458711036871,-21.0459107956361,
7.69413644759044));
#174374=CARTESIAN_POINT('Ctrl Pts',(19.0518866226705,-21.0450059960072,
7.69377141708849));
#174375=CARTESIAN_POINT('Ctrl Pts',(19.0662768248414,-21.0427780841774,
7.69289563764516));
#174376=CARTESIAN_POINT('Ctrl Pts',(19.0746475740017,-21.0414305713898,
7.69238411877348));
#174377=CARTESIAN_POINT('Ctrl Pts',(19.1049386345306,-21.0363674899412,
7.69052542608143));
#174378=CARTESIAN_POINT('Ctrl Pts',(19.1268075698795,-21.0323570505082,
7.68916892989207));
#174379=CARTESIAN_POINT('Ctrl Pts',(19.3293697769554,-20.9919023681982,
7.67646415885305));
#174380=CARTESIAN_POINT('Ctrl Pts',(19.5046095698364,-20.9323536748864,
7.66432894762078));
#174381=CARTESIAN_POINT('Ctrl Pts',(19.7425292966968,-20.8150933724153,
7.64681469631331));
#174382=CARTESIAN_POINT('Ctrl Pts',(19.8130652399463,-20.7751478843502,
7.64149137483685));
#174383=CARTESIAN_POINT('Ctrl Pts',(19.9116141894632,-20.7116102705018,
7.63401527075843));
#174384=CARTESIAN_POINT('Ctrl Pts',(19.9415782464914,-20.6911833216775,
7.63173707279578));
#174385=CARTESIAN_POINT('Ctrl Pts',(19.9770748889911,-20.6656247458028,
7.62904596747366));
#174386=CARTESIAN_POINT('Ctrl Pts',(19.9831219110962,-20.6612218709477,
7.62858780578386));
#174387=CARTESIAN_POINT('Ctrl Pts',(19.9924973882524,-20.6543191969485,
7.62787806211732));
#174388=CARTESIAN_POINT('Ctrl Pts',(19.9958419518017,-20.6518415261133,
7.62762499202941));
#174389=CARTESIAN_POINT('Ctrl Pts',(20.0020379817709,-20.6472231091899,
7.62715642092181));
#174390=CARTESIAN_POINT('Ctrl Pts',(20.0048913206027,-20.6450850435348,
7.6269407450377));
#174391=CARTESIAN_POINT('Ctrl Pts',(20.0113387267232,-20.6402283863224,
7.62645363115794));
#174392=CARTESIAN_POINT('Ctrl Pts',(20.0149295140985,-20.637505528898,7.62618249709004));
#174393=CARTESIAN_POINT('Ctrl Pts',(20.0257622304005,-20.6292365794639,
7.62536492091644));
#174394=CARTESIAN_POINT('Ctrl Pts',(20.0329771437777,-20.6236550451822,
7.62482091120557));
#174395=CARTESIAN_POINT('Ctrl Pts',(20.0884445674614,-20.5801688919378,
7.62064071834189));
#174396=CARTESIAN_POINT('Ctrl Pts',(20.1350693845819,-20.5402254539061,
7.61713897371162));
#174397=CARTESIAN_POINT('Ctrl Pts',(20.2871671507481,-20.3980043852527,
7.60550202522887));
#174398=CARTESIAN_POINT('Ctrl Pts',(20.3837128764582,-20.2868066810572,
7.59771463143669));
#174399=CARTESIAN_POINT('Ctrl Pts',(20.5211894319472,-20.090528536099,7.58451611416308));
#174400=CARTESIAN_POINT('Ctrl Pts',(20.5693480780316,-20.0111448654155,
7.57930756107859));
#174401=CARTESIAN_POINT('Ctrl Pts',(20.6218684703958,-19.9101679373517,
7.57267773484364));
#174402=CARTESIAN_POINT('Ctrl Pts',(20.631313294231,-19.8913270857248,7.57144083723901));
#174403=CARTESIAN_POINT('Ctrl Pts',(20.6443685992348,-19.8642834134045,
7.56966428738855));
#174404=CARTESIAN_POINT('Ctrl Pts',(20.6482109146407,-19.8561934427054,
7.56913270131874));
#174405=CARTESIAN_POINT('Ctrl Pts',(20.6547601154102,-19.8421752897911,
7.56821123358712));
#174406=CARTESIAN_POINT('Ctrl Pts',(20.6574911942651,-19.8362584981922,
7.56782219454299));
#174407=CARTESIAN_POINT('Ctrl Pts',(20.6626743627559,-19.8248916983921,
7.5670745673735));
#174408=CARTESIAN_POINT('Ctrl Pts',(20.6651307823195,-19.819443724465,7.56671613300442));
#174409=CARTESIAN_POINT('Ctrl Pts',(20.6714718854522,-19.8052196687878,
7.56577998895957));
#174410=CARTESIAN_POINT('Ctrl Pts',(20.6753199833069,-19.7964275148245,
7.56520103251628));
#174411=CARTESIAN_POINT('Ctrl Pts',(20.6883056550384,-19.7661998401453,
7.56320933242042));
#174412=CARTESIAN_POINT('Ctrl Pts',(20.6971487798813,-19.7446403806079,
7.56178664609279));
#174413=CARTESIAN_POINT('Ctrl Pts',(20.7678888704943,-19.5637267355981,
7.54982644524309));
#174414=CARTESIAN_POINT('Ctrl Pts',(20.8106183403783,-19.3975873328279,
7.53862561343313));
#174415=CARTESIAN_POINT('Ctrl Pts',(20.8446804915029,-19.1387026609447,
7.52137064430835));
#174416=CARTESIAN_POINT('Ctrl Pts',(20.850720204172,-19.0485794585914,7.51541603746372));
#174417=CARTESIAN_POINT('Ctrl Pts',(20.8511061996304,-18.9197162415058,
7.50718304618558));
#174418=CARTESIAN_POINT('Ctrl Pts',(20.8501647981973,-18.8810924327384,
7.50475213048953));
#174419=CARTESIAN_POINT('Ctrl Pts',(20.8477729663797,-18.8349065986079,
7.50190597659676));
#174420=CARTESIAN_POINT('Ctrl Pts',(20.8473379761702,-18.8273018822425,
7.50143932087353));
#174421=CARTESIAN_POINT('Ctrl Pts',(20.8465999633302,-18.8155156848552,
7.50071931190345));
#174422=CARTESIAN_POINT('Ctrl Pts',(20.8463255543148,-18.8113325672559,
7.50046440174732));
#174423=CARTESIAN_POINT('Ctrl Pts',(20.8457949348328,-18.8035956612786,
7.49999413736087));
#174424=CARTESIAN_POINT('Ctrl Pts',(20.8455421805573,-18.8000417341095,
7.49977859742441));
#174425=CARTESIAN_POINT('Ctrl Pts',(20.8449522838862,-18.7920330895462,
7.49929394487906));
#174426=CARTESIAN_POINT('Ctrl Pts',(20.844610013377,-18.7875788044112,7.49902512302226));
#174427=CARTESIAN_POINT('Ctrl Pts',(20.8435638848998,-18.7745063891234,
7.49823825540963));
#174428=CARTESIAN_POINT('Ctrl Pts',(20.8428213141118,-18.7658913292997,
7.49772233096261));
#174429=CARTESIAN_POINT('Ctrl Pts',(20.8372749449805,-18.7058464243521,
7.49414339381277));
#174430=CARTESIAN_POINT('Ctrl Pts',(20.8306426326194,-18.6545984492913,
7.49117536667984));
#174431=CARTESIAN_POINT('Ctrl Pts',(20.8185581711124,-18.582161657239,7.48703946443716));
#174432=CARTESIAN_POINT('Ctrl Pts',(20.8146436848486,-18.5607391274452,
7.48582377721568));
#174433=CARTESIAN_POINT('Ctrl Pts',(20.80140135268,-18.4941005975533,7.48205535319941));
#174434=CARTESIAN_POINT('Ctrl Pts',(20.7909244439018,-18.4491259666275,
7.47953088872672));
#174435=CARTESIAN_POINT('Ctrl Pts',(20.7507051679,-18.2988937538901,7.47106355920194));
#174436=CARTESIAN_POINT('Ctrl Pts',(20.7142829501654,-18.1956098512443,
7.46517521627707));
#174437=CARTESIAN_POINT('Ctrl Pts',(20.647750716248,-18.0452006831621,7.45603029254469));
#174438=CARTESIAN_POINT('Ctrl Pts',(20.6234958509789,-17.9956885504537,
7.45292243941184));
#174439=CARTESIAN_POINT('Ctrl Pts',(20.581052886092,-17.9169822014336,7.44777792058188));
#174440=CARTESIAN_POINT('Ctrl Pts',(20.5640366625488,-17.8871846054571,
7.44578065273709));
#174441=CARTESIAN_POINT('Ctrl Pts',(20.540717737575,-17.8485613490703,7.44311982723011));
#174442=CARTESIAN_POINT('Ctrl Pts',(20.5350602037008,-17.8393509197776,
7.44247980191957));
#174443=CARTESIAN_POINT('Ctrl Pts',(20.5256770234057,-17.8243342562632,
7.44142707182663));
#174444=CARTESIAN_POINT('Ctrl Pts',(20.5219930481673,-17.8185021200854,
7.44101590846227));
#174445=CARTESIAN_POINT('Ctrl Pts',(20.5148057904764,-17.8072461282298,
7.44021783758158));
#174446=CARTESIAN_POINT('Ctrl Pts',(20.5113060651323,-17.801820083753,7.43983106547224));
#174447=CARTESIAN_POINT('Ctrl Pts',(20.5031665829805,-17.7893263221723,
7.43893569814861));
#174448=CARTESIAN_POINT('Ctrl Pts',(20.4985092235669,-17.7822702550774,
7.43842644685737));
#174449=CARTESIAN_POINT('Ctrl Pts',(20.4858668730179,-17.7633639559323,
7.43705217979012));
#174450=CARTESIAN_POINT('Ctrl Pts',(20.4778040672908,-17.7515665177865,
7.43618423622166));
#174451=CARTESIAN_POINT('Ctrl Pts',(20.40274250566,-17.6440891103439,7.42817965058385));
#174452=CARTESIAN_POINT('Ctrl Pts',(20.3280628868999,-17.5540414314203,
7.4207414655405));
#174453=CARTESIAN_POINT('Ctrl Pts',(20.1325800273237,-17.3544713805741,
7.40249414441274));
#174454=CARTESIAN_POINT('Ctrl Pts',(20.005810433897,-17.251817052567,7.39154529268232));
#174455=CARTESIAN_POINT('Ctrl Pts',(19.8409604834936,-17.1471745792833,
7.37913630684207));
#174456=CARTESIAN_POINT('Ctrl Pts',(19.8129750486933,-17.1303058906809,
7.37708848181603));
#174457=CARTESIAN_POINT('Ctrl Pts',(19.7783138750587,-17.1104924376088,
7.37463335252583));
#174458=CARTESIAN_POINT('Ctrl Pts',(19.7720005474634,-17.1069264407745,
7.37418939548587));
#174459=CARTESIAN_POINT('Ctrl Pts',(19.7620781525388,-17.1013889599327,
7.3734968452897));
#174460=CARTESIAN_POINT('Ctrl Pts',(19.7584815194936,-17.0993954749522,
7.37324687611266));
#174461=CARTESIAN_POINT('Ctrl Pts',(19.7517502349969,-17.0956901618897,
7.37278106367706));
#174462=CARTESIAN_POINT('Ctrl Pts',(19.7486170944442,-17.0939758053795,
7.37256506405661));
#174463=CARTESIAN_POINT('Ctrl Pts',(19.741458172694,-17.090082175408,7.37207337135263));
#174464=CARTESIAN_POINT('Ctrl Pts',(19.7374296600905,-17.0879080297863,
7.37179800622117));
#174465=CARTESIAN_POINT('Ctrl Pts',(19.725036134151,-17.0812711932295,7.37095481735169));
#174466=CARTESIAN_POINT('Ctrl Pts',(19.7166480362049,-17.0768515439621,
7.37038965572208));
#174467=CARTESIAN_POINT('Ctrl Pts',(19.6008142323478,-17.0168099874429,
7.36265695354855));
#174468=CARTESIAN_POINT('Ctrl Pts',(19.4888059357739,-16.9704339864077,
7.35601945711191));
#174469=CARTESIAN_POINT('Ctrl Pts',(19.2028079839835,-16.8798165665215,
7.33969350389045));
#174470=CARTESIAN_POINT('Ctrl Pts',(19.0260364714918,-16.8476158197381,
7.33007481375237));
#174471=CARTESIAN_POINT('Ctrl Pts',(18.8258763910339,-16.8368855460631,
7.31840384695642));
#174472=CARTESIAN_POINT('Ctrl Pts',(18.8044107491275,-16.8360622171434,
7.31714349183365));
#174473=CARTESIAN_POINT('Ctrl Pts',(18.7739144147734,-16.8353570713255,
7.315339102029));
#174474=CARTESIAN_POINT('Ctrl Pts',(18.7648908377787,-16.8352061507281,
7.31480348852575));
#174475=CARTESIAN_POINT('Ctrl Pts',(18.7493378582586,-16.8350454940832,
7.31387725390126));
#174476=CARTESIAN_POINT('Ctrl Pts',(18.7428088200906,-16.8350082585817,
7.31348749923424));
#174477=CARTESIAN_POINT('Ctrl Pts',(18.7303180279547,-16.834994807401,7.31274004039551));
#174478=CARTESIAN_POINT('Ctrl Pts',(18.7243563334241,-16.8350135709045,
7.31238249740935));
#174479=CARTESIAN_POINT('Ctrl Pts',(18.7088771926739,-16.8351276762229,
7.31145207142552));
#174480=CARTESIAN_POINT('Ctrl Pts',(18.6993602462997,-16.8352620205945,
7.31087797149548));
#174481=CARTESIAN_POINT('Ctrl Pts',(18.6670303152539,-16.8359364892103,
7.30892055874067));
#174482=CARTESIAN_POINT('Ctrl Pts',(18.6442259049728,-16.8367812717643,
7.30752775950298));
#174483=CARTESIAN_POINT('Ctrl Pts',(18.4439242482592,-16.8474462853925,
7.2951834561723));
#174484=CARTESIAN_POINT('Ctrl Pts',(18.268337319563,-16.8792182421591,7.28350740653347));
#174485=CARTESIAN_POINT('Ctrl Pts',(18.0173334357542,-16.9581655260814,
7.26612446145114));
#174486=CARTESIAN_POINT('Ctrl Pts',(17.9374624013684,-16.9887077134318,
7.26049815820106));
#174487=CARTESIAN_POINT('Ctrl Pts',(17.8255729342821,-17.0394494914775,
7.25265696252434));
#174488=CARTESIAN_POINT('Ctrl Pts',(17.7919077540756,-17.0558059752339,
7.250303840077));
#174489=CARTESIAN_POINT('Ctrl Pts',(17.7519919183697,-17.076525098068,7.24753653630727));
#174490=CARTESIAN_POINT('Ctrl Pts',(17.7453107276195,-17.0800385936707,
7.24707412250526));
#174491=CARTESIAN_POINT('Ctrl Pts',(17.7349616587644,-17.085551811115,7.24635923847559));
#174492=CARTESIAN_POINT('Ctrl Pts',(17.7312807434474,-17.087526738651,7.24610524586216));
#174493=CARTESIAN_POINT('Ctrl Pts',(17.7244699970279,-17.0912069227537,
7.24563583071761));
#174494=CARTESIAN_POINT('Ctrl Pts',(17.7213386544485,-17.0929091730773,
7.24542022787485));
#174495=CARTESIAN_POINT('Ctrl Pts',(17.7142752475803,-17.0967721007728,
7.24493437020623));
#174496=CARTESIAN_POINT('Ctrl Pts',(17.7103457550295,-17.0989373684697,
7.24466441260949));
#174497=CARTESIAN_POINT('Ctrl Pts',(17.6987856658911,-17.1053553150359,
7.24387112546098));
#174498=CARTESIAN_POINT('Ctrl Pts',(17.6911743668109,-17.1096428102119,
7.24334996948272));
#174499=CARTESIAN_POINT('Ctrl Pts',(17.6369037156688,-17.1406579084608,
7.23964068144928));
#174500=CARTESIAN_POINT('Ctrl Pts',(17.591246918417,-17.1691099680363,7.23655557857932));
#174501=CARTESIAN_POINT('Ctrl Pts',(17.4071719508445,-17.293800556916,7.22405649839376));
#174502=CARTESIAN_POINT('Ctrl Pts',(17.2794064967081,-17.4046591977115,
7.21518662745224));
#174503=CARTESIAN_POINT('Ctrl Pts',(17.111546472248,-17.5896734100594,7.20134224817517));
#174504=CARTESIAN_POINT('Ctrl Pts',(17.0604711081228,-17.6529279660675,
7.19675114253332));
#174505=CARTESIAN_POINT('Ctrl Pts',(17.0017259821591,-17.7349128743434,
7.19086729246939));
#174506=CARTESIAN_POINT('Ctrl Pts',(16.9905151964005,-17.7510274584236,
7.18971400672685));
#174507=CARTESIAN_POINT('Ctrl Pts',(16.974659743329,-17.7745083382265,7.1880370588382));
#174508=CARTESIAN_POINT('Ctrl Pts',(16.9698336762098,-17.7817513380291,
7.18752025935566));
#174509=CARTESIAN_POINT('Ctrl Pts',(16.9614964374229,-17.7944327137419,
7.18661615870344));
#174510=CARTESIAN_POINT('Ctrl Pts',(16.9579652679746,-17.7998578513191,
7.18622961375325));
#174511=CARTESIAN_POINT('Ctrl Pts',(16.9511894724408,-17.8103730650232,
7.18548080646452));
#174512=CARTESIAN_POINT('Ctrl Pts',(16.947941622299,-17.8154609966607,7.18511866932175));
#174513=CARTESIAN_POINT('Ctrl Pts',(16.9402801559074,-17.8275770391311,
7.18425670132761));
#174514=CARTESIAN_POINT('Ctrl Pts',(16.9358860442713,-17.8346173112282,
7.18375615460599));
#174515=CARTESIAN_POINT('Ctrl Pts',(16.9204543816215,-17.8596687687294,
7.18197605638755));
#174516=CARTESIAN_POINT('Ctrl Pts',(16.9096454223261,-17.8778186592026,
7.1806881747611));
#174517=CARTESIAN_POINT('Ctrl Pts',(16.8384380928337,-18.0015623051455,
7.17191696790891));
#174518=CARTESIAN_POINT('Ctrl Pts',(16.7870403110365,-18.1119034699418,
7.16412181699196));
#174519=CARTESIAN_POINT('Ctrl Pts',(16.7454193236514,-18.2258898887546,
7.15616137122351));
#174520=CARTESIAN_POINT('',(16.620190946188,-18.9524614545077,7.68893946617128));
#174521=CARTESIAN_POINT('Ctrl Pts',(16.6203930087273,-18.9524685809736,
7.68905589348695));
#174522=CARTESIAN_POINT('Ctrl Pts',(16.6197601590257,-19.2779557757106,
7.66955339595332));
#174523=CARTESIAN_POINT('Ctrl Pts',(16.8436653962077,-20.3101166792811,
7.60765896285921));
#174524=CARTESIAN_POINT('Ctrl Pts',(18.4531255376191,-21.4394563861295,
7.50337259420462));
#174525=CARTESIAN_POINT('Ctrl Pts',(20.673525152946,-20.5345839369853,7.3761967875232));
#174526=CARTESIAN_POINT('Ctrl Pts',(21.1145308209525,-18.1777889518937,
7.24902098084176));
#174527=CARTESIAN_POINT('Ctrl Pts',(19.371547213141,-16.5312845504829,7.12184517416032));
#174528=CARTESIAN_POINT('Ctrl Pts',(17.4471161563804,-17.0060916441732,
7.01671104281645));
#174529=CARTESIAN_POINT('Ctrl Pts',(16.8648290660527,-17.9078853718336,
6.95396884703307));
#174530=CARTESIAN_POINT('Ctrl Pts',(16.7486737197731,-18.2270709325543,
6.93361858681016));
#174531=CARTESIAN_POINT('Ctrl Pts',(16.6170000287534,-18.9523489152706,
7.68710087722452));
#174532=CARTESIAN_POINT('Ctrl Pts',(16.6169985639086,-18.9434611516821,
7.68762144269225));
#174533=CARTESIAN_POINT('Ctrl Pts',(16.6170530690849,-18.9345735467869,
7.68814369652498));
#174534=CARTESIAN_POINT('Ctrl Pts',(16.617270741598,-18.9170624098664,7.6891761672149));
#174535=CARTESIAN_POINT('Ctrl Pts',(16.6174306467703,-18.9084390286407,
7.68968627225728));
#174536=CARTESIAN_POINT('Ctrl Pts',(16.6177963854143,-18.8936059821696,
7.69056666148997));
#174537=CARTESIAN_POINT('Ctrl Pts',(16.6179768690861,-18.8873957595661,
7.69093615093166));
#174538=CARTESIAN_POINT('Ctrl Pts',(16.6183911393856,-18.8750179065797,
7.69167441356522));
#174539=CARTESIAN_POINT('Ctrl Pts',(16.6186245666237,-18.8688503250775,
7.6920431719162));
#174540=CARTESIAN_POINT('Ctrl Pts',(16.6191442764769,-18.8565429565483,
7.69278085784545));
#174541=CARTESIAN_POINT('Ctrl Pts',(16.6194303341952,-18.8504032201223,
7.69314977482355));
#174542=CARTESIAN_POINT('Ctrl Pts',(16.6202771216525,-18.8337853709109,
7.6941507934745));
#174543=CARTESIAN_POINT('Ctrl Pts',(16.620889018733,-18.8233101417259,7.69478449461903));
#174544=CARTESIAN_POINT('Ctrl Pts',(16.6234852736034,-18.7838994956495,
7.69717905954279));
#174545=CARTESIAN_POINT('Ctrl Pts',(16.6259862430238,-18.7550023876169,
7.69895602655921));
#174546=CARTESIAN_POINT('Ctrl Pts',(16.6474328530892,-18.555105247614,7.71140127744809));
#174547=CARTESIAN_POINT('Ctrl Pts',(16.6865510291809,-18.3871110626015,
7.72271575218188));
#174548=CARTESIAN_POINT('Ctrl Pts',(16.7454193803189,-18.2258897335605,
7.7340522080425));
#174549=CARTESIAN_POINT('Origin',(18.734,-18.952,0.));
#174550=CARTESIAN_POINT('',(16.7454192490578,-18.2258900930424,8.75434673926218));
#174551=CARTESIAN_POINT('',(16.74541940036,-18.2258896786745,8.53521106622902));
#174552=CARTESIAN_POINT('',(16.7454193692319,-18.2258897639242,0.));
#174553=CARTESIAN_POINT('Ctrl Pts',(16.7454192490578,-18.2258900930424,
8.75434673926218));
#174554=CARTESIAN_POINT('Ctrl Pts',(16.7157810160982,-18.3070596501447,
8.74958602597419));
#174555=CARTESIAN_POINT('Ctrl Pts',(16.6911130922396,-18.3900421657471,
8.74492440772906));
#174556=CARTESIAN_POINT('Ctrl Pts',(16.6409703506581,-18.6065647959986,
8.73282224506912));
#174557=CARTESIAN_POINT('Ctrl Pts',(16.6231411488845,-18.741366281552,8.72532552821618));
#174558=CARTESIAN_POINT('Ctrl Pts',(16.6177334387486,-18.8937846281362,
8.71640095673513));
#174559=CARTESIAN_POINT('Ctrl Pts',(16.6173369769236,-18.9106380599995,
8.7154084548658));
#174560=CARTESIAN_POINT('Ctrl Pts',(16.6170471059385,-18.935677546351,8.71392476474412));
#174561=CARTESIAN_POINT('Ctrl Pts',(16.6169998255506,-18.9438614082098,
8.71343839415166));
#174562=CARTESIAN_POINT('Ctrl Pts',(16.6170001372493,-18.9584435198302,
8.71256912102238));
#174563=CARTESIAN_POINT('Ctrl Pts',(16.6170292805039,-18.9648416993522,
8.71218680132263));
#174564=CARTESIAN_POINT('Ctrl Pts',(16.6171518843144,-18.9783316689556,
8.71137875762645));
#174565=CARTESIAN_POINT('Ctrl Pts',(16.6172519794822,-18.985423306241,8.71095283028561));
#174566=CARTESIAN_POINT('Ctrl Pts',(16.6176113756808,-19.0041994799665,
8.70982204028203));
#174567=CARTESIAN_POINT('Ctrl Pts',(16.6179318028016,-19.0158824786473,
8.7091152711121));
#174568=CARTESIAN_POINT('Ctrl Pts',(16.619877996158,-19.0703736724706,8.70580362709433));
#174569=CARTESIAN_POINT('Ctrl Pts',(16.6227060712927,-19.1131263516106,
8.7031613837008));
#174570=CARTESIAN_POINT('Ctrl Pts',(16.6340979487179,-19.2309338546192,
8.69575360055693));
#174571=CARTESIAN_POINT('Ctrl Pts',(16.645383694069,-19.3056561876156,8.69090978752918));
#174572=CARTESIAN_POINT('Ctrl Pts',(16.6865619595508,-19.5053184250742,
8.67762193844367));
#174573=CARTESIAN_POINT('Ctrl Pts',(16.7238652491619,-19.6284024291809,
8.66904373553352));
#174574=CARTESIAN_POINT('Ctrl Pts',(16.7783254108682,-19.7627415339463,
8.65959210382905));
#174575=CARTESIAN_POINT('Ctrl Pts',(16.7847472716301,-19.7780621979819,
8.65851318248265));
#174576=CARTESIAN_POINT('Ctrl Pts',(16.8125068973829,-19.8421616690798,
8.65399898355628));
#174577=CARTESIAN_POINT('Ctrl Pts',(16.8355023896456,-19.8902064779321,
8.65061472602623));
#174578=CARTESIAN_POINT('Ctrl Pts',(16.8643428448303,-19.9450493699819,
8.64679237499746));
#174579=CARTESIAN_POINT('Ctrl Pts',(16.8684462246156,-19.9527367517207,
8.64625755796771));
#174580=CARTESIAN_POINT('Ctrl Pts',(16.8747318708117,-19.9643394245033,
8.64545207073187));
#174581=CARTESIAN_POINT('Ctrl Pts',(16.8768792398725,-19.9682733735453,
8.64517926733447));
#174582=CARTESIAN_POINT('Ctrl Pts',(16.8807565447678,-19.9753232121195,
8.64469097276679));
#174583=CARTESIAN_POINT('Ctrl Pts',(16.8824818622009,-19.9784415652183,
8.64447519392715));
#174584=CARTESIAN_POINT('Ctrl Pts',(16.8862483303803,-19.9852087139538,
8.64400738909291));
#174585=CARTESIAN_POINT('Ctrl Pts',(16.888292411181,-19.9888558127542,8.64375555448036));
#174586=CARTESIAN_POINT('Ctrl Pts',(16.8940655242946,-19.9990851713286,
8.64304994399046));
#174587=CARTESIAN_POINT('Ctrl Pts',(16.8978190974434,-20.0056536090705,
8.64259771630789));
#174588=CARTESIAN_POINT('Ctrl Pts',(16.9204917409967,-20.0448397054969,
8.63990408704711));
#174589=CARTESIAN_POINT('Ctrl Pts',(16.9402455788541,-20.0769694662312,
8.63771329709888));
#174590=CARTESIAN_POINT('Ctrl Pts',(17.0081344025204,-20.1810518571699,
8.63061758543766));
#174591=CARTESIAN_POINT('Ctrl Pts',(17.0598256572541,-20.250585063833,8.62587708537816));
#174592=CARTESIAN_POINT('Ctrl Pts',(17.2291736386244,-20.4514018409526,
8.61158243682669));
#174593=CARTESIAN_POINT('Ctrl Pts',(17.3590568528564,-20.5713310132791,
8.60211687602608));
#174594=CARTESIAN_POINT('Ctrl Pts',(17.5209474976524,-20.6871423988481,
8.59054985572336));
#174595=CARTESIAN_POINT('Ctrl Pts',(17.5398251033512,-20.7001881401564,
8.58920551242383));
#174596=CARTESIAN_POINT('Ctrl Pts',(17.5668448400371,-20.7182187916646,
8.58728582490246));
#174597=CARTESIAN_POINT('Ctrl Pts',(17.5748147687717,-20.7234597321511,
8.58672012596513));
#174598=CARTESIAN_POINT('Ctrl Pts',(17.5878261733346,-20.7318904871905,
8.5857973509874));
#174599=CARTESIAN_POINT('Ctrl Pts',(17.5928462491103,-20.7351132053329,
8.58544150799897));
#174600=CARTESIAN_POINT('Ctrl Pts',(17.6033863050286,-20.7418168228078,
8.58469473570081));
#174601=CARTESIAN_POINT('Ctrl Pts',(17.608908885671,-20.7452934978525,8.58430365480356));
#174602=CARTESIAN_POINT('Ctrl Pts',(17.6220914693385,-20.7535075735396,
8.58337055818764));
#174603=CARTESIAN_POINT('Ctrl Pts',(17.629765756773,-20.7582217057285,8.58282769275946));
#174604=CARTESIAN_POINT('Ctrl Pts',(17.6557517539132,-20.7739567769158,
8.58099048444875));
#174605=CARTESIAN_POINT('Ctrl Pts',(17.6741997456372,-20.7847490677745,
8.57968785099279));
#174606=CARTESIAN_POINT('Ctrl Pts',(17.7757283767702,-20.8420990125517,
8.57252537896947));
#174607=CARTESIAN_POINT('Ctrl Pts',(17.8617042598789,-20.883283172637,8.56647650732707));
#174608=CARTESIAN_POINT('Ctrl Pts',(18.1086077821844,-20.981697404587,8.5492049106827));
#174609=CARTESIAN_POINT('Ctrl Pts',(18.2741076234026,-21.0254712030293,
8.53769532032363));
#174610=CARTESIAN_POINT('Ctrl Pts',(18.4795036363772,-21.0539691283966,
8.52446036907041));
#174611=CARTESIAN_POINT('Ctrl Pts',(18.5160742971354,-21.0580748754707,
8.52214606145962));
#174612=CARTESIAN_POINT('Ctrl Pts',(18.5598516626819,-21.061837047248,8.51944030043692));
#174613=CARTESIAN_POINT('Ctrl Pts',(18.5669706811736,-21.0624125708737,
8.51900232918123));
#174614=CARTESIAN_POINT('Ctrl Pts',(18.5785920842403,-21.0632929075178,
8.51829083659204));
#174615=CARTESIAN_POINT('Ctrl Pts',(18.5830927043418,-21.0636193668852,
8.51801614566152));
#174616=CARTESIAN_POINT('Ctrl Pts',(18.5911518109754,-21.0641780490793,
8.51752582701449));
#174617=CARTESIAN_POINT('Ctrl Pts',(18.594709859013,-21.0644156724828,8.51730990110314));
#174618=CARTESIAN_POINT('Ctrl Pts',(18.6024178398849,-21.0649108884691,
8.51684331964734));
#174619=CARTESIAN_POINT('Ctrl Pts',(18.6065679231275,-21.0651652452988,
8.51659284717148));
#174620=CARTESIAN_POINT('Ctrl Pts',(18.6181655874626,-21.0658417709624,
8.51589489080486));
#174621=CARTESIAN_POINT('Ctrl Pts',(18.6256147748996,-21.066236810419,8.51544890158573));
#174622=CARTESIAN_POINT('Ctrl Pts',(18.6689430807067,-21.0683049622748,
8.51286741728908));
#174623=CARTESIAN_POINT('Ctrl Pts',(18.7048603489582,-21.0691042304372,
8.51077775520912));
#174624=CARTESIAN_POINT('Ctrl Pts',(18.8205143230973,-21.0687336723076,
8.50416145657084));
#174625=CARTESIAN_POINT('Ctrl Pts',(18.9001742030535,-21.0639740260526,
8.49977486958345));
#174626=CARTESIAN_POINT('Ctrl Pts',(19.1643321808389,-21.033147756535,8.48527488305165));
#174627=CARTESIAN_POINT('Ctrl Pts',(19.3456060267506,-20.987262607043,8.47531870978353));
#174628=CARTESIAN_POINT('Ctrl Pts',(19.5390171582457,-20.9100915444266,
8.46320679728048));
#174629=CARTESIAN_POINT('Ctrl Pts',(19.5593659222989,-20.9016015392574,
8.46191427218898));
#174630=CARTESIAN_POINT('Ctrl Pts',(19.5873242460484,-20.8894204832188,
8.46011152219675));
#174631=CARTESIAN_POINT('Ctrl Pts',(19.5950503025094,-20.8859991652254,
8.45961047622032));
#174632=CARTESIAN_POINT('Ctrl Pts',(19.6082960307969,-20.880038475588,8.45874643662393));
#174633=CARTESIAN_POINT('Ctrl Pts',(19.6138256722399,-20.8775214094106,
8.45838421117874));
#174634=CARTESIAN_POINT('Ctrl Pts',(19.6252035963097,-20.8722829889565,
8.45763571584839));
#174635=CARTESIAN_POINT('Ctrl Pts',(19.631050423789,-20.8695586414769,8.45724934557353));
#174636=CARTESIAN_POINT('Ctrl Pts',(19.6446285239896,-20.8631561924117,
8.45634798178006));
#174637=CARTESIAN_POINT('Ctrl Pts',(19.6523500760168,-20.8594578461956,
8.45583229000792));
#174638=CARTESIAN_POINT('Ctrl Pts',(19.6769969751317,-20.8474685200703,
8.454176124448));
#174639=CARTESIAN_POINT('Ctrl Pts',(19.6938337578429,-20.8389984968026,
8.45302942603647));
#174640=CARTESIAN_POINT('Ctrl Pts',(19.7773927470935,-20.795555109936,8.44725982575586));
#174641=CARTESIAN_POINT('Ctrl Pts',(19.8423209852681,-20.7572662662378,
8.44252053346244));
#174642=CARTESIAN_POINT('Ctrl Pts',(19.9960070390426,-20.6552158438107,
8.43066518235256));
#174643=CARTESIAN_POINT('Ctrl Pts',(20.0821353815349,-20.5878892072224,
8.42344928725966));
#174644=CARTESIAN_POINT('Ctrl Pts',(20.173122420313,-20.504680215372,8.41530416857833));
#174645=CARTESIAN_POINT('Ctrl Pts',(20.1834675881393,-20.4950271889208,
8.41436997166442));
#174646=CARTESIAN_POINT('Ctrl Pts',(20.269508973462,-20.4131134830144,8.40653561155425));
#174647=CARTESIAN_POINT('Ctrl Pts',(20.3398574719983,-20.3354259662255,
8.39969810472665));
#174648=CARTESIAN_POINT('Ctrl Pts',(20.4101290099512,-20.2452031417365,
8.39263251411188));
#174649=CARTESIAN_POINT('Ctrl Pts',(20.4160285993265,-20.2375203705226,
8.39203736458283));
#174650=CARTESIAN_POINT('Ctrl Pts',(20.4246626345543,-20.2261154501457,
8.39116377634351));
#174651=CARTESIAN_POINT('Ctrl Pts',(20.4274378694937,-20.2224245382058,
8.39088257730593));
#174652=CARTESIAN_POINT('Ctrl Pts',(20.4323404553899,-20.2158597555363,
8.39038515391424));
#174653=CARTESIAN_POINT('Ctrl Pts',(20.4344726226762,-20.2129895496339,
8.39016859523483));
#174654=CARTESIAN_POINT('Ctrl Pts',(20.4390258794515,-20.2068276560915,
8.38970565670783));
#174655=CARTESIAN_POINT('Ctrl Pts',(20.4414447069695,-20.2035343660414,
8.38945943343401));
#174656=CARTESIAN_POINT('Ctrl Pts',(20.448059518757,-20.194473275021,8.38878520297246));
#174657=CARTESIAN_POINT('Ctrl Pts',(20.4522359574534,-20.1886911784249,
8.38835852996528));
#174658=CARTESIAN_POINT('Ctrl Pts',(20.4743977322523,-20.1576801782317,
8.38608852389913));
#174659=CARTESIAN_POINT('Ctrl Pts',(20.4918578235873,-20.1320784122042,
8.38427905887846));
#174660=CARTESIAN_POINT('Ctrl Pts',(20.5979099846711,-19.9689937939593,
8.37309021314127));
#174661=CARTESIAN_POINT('Ctrl Pts',(20.6708907465366,-19.822001949655,8.3644462344041));
#174662=CARTESIAN_POINT('Ctrl Pts',(20.7660349872544,-19.5572910783922,
8.34905144674781));
#174663=CARTESIAN_POINT('Ctrl Pts',(20.7965356025286,-19.4434112557633,
8.34248333727952));
#174664=CARTESIAN_POINT('Ctrl Pts',(20.8199519372763,-19.3135218283323,
8.33475142543334));
#174665=CARTESIAN_POINT('Ctrl Pts',(20.8223464710435,-19.2994226804983,
8.33390927611133));
#174666=CARTESIAN_POINT('Ctrl Pts',(20.8259295438054,-19.2769481804365,
8.33256186165773));
#174667=CARTESIAN_POINT('Ctrl Pts',(20.8272110756077,-19.2685879435499,
8.33205954349965));
#174668=CARTESIAN_POINT('Ctrl Pts',(20.8293826061142,-19.2538317932811,
8.33117091255808));
#174669=CARTESIAN_POINT('Ctrl Pts',(20.8302935087911,-19.2474390309615,
8.33078526685305));
#174670=CARTESIAN_POINT('Ctrl Pts',(20.8321168000064,-19.2342099582484,
8.32998579914036));
#174671=CARTESIAN_POINT('Ctrl Pts',(20.8330250559964,-19.2273731641823,
8.32957185131814));
#174672=CARTESIAN_POINT('Ctrl Pts',(20.8352701963922,-19.2098163441194,
8.32850677519392));
#174673=CARTESIAN_POINT('Ctrl Pts',(20.8365584494455,-19.1990903993113,
8.32785411979507));
#174674=CARTESIAN_POINT('Ctrl Pts',(20.8415891532997,-19.1543128121803,
8.32512097083759));
#174675=CARTESIAN_POINT('Ctrl Pts',(20.8445867308715,-19.1201842714433,
8.32301720800361));
#174676=CARTESIAN_POINT('Ctrl Pts',(20.8502360494753,-19.0311121246598,
8.31746979021053));
#174677=CARTESIAN_POINT('Ctrl Pts',(20.851576785722,-18.9761140106063,8.3139878713536));
#174678=CARTESIAN_POINT('Ctrl Pts',(20.8491809905767,-18.8118350162185,
8.30342826234796));
#174679=CARTESIAN_POINT('Ctrl Pts',(20.8391247986837,-18.7028354774673,
8.2962021486675));
#174680=CARTESIAN_POINT('Ctrl Pts',(20.8141516884167,-18.5568204474596,
8.28641655421683));
#174681=CARTESIAN_POINT('Ctrl Pts',(20.8065503686207,-18.5187183361101,
8.28385447449473));
#174682=CARTESIAN_POINT('Ctrl Pts',(20.7915455180272,-18.4529890664879,
8.27943831844381));
#174683=CARTESIAN_POINT('Ctrl Pts',(20.7846226373766,-18.425262527147,8.27757664320697));
#174684=CARTESIAN_POINT('Ctrl Pts',(20.7634343267692,-18.3471650462427,
8.27235015105871));
#174685=CARTESIAN_POINT('Ctrl Pts',(20.7478579873175,-18.2971671965401,
8.26902454029946));
#174686=CARTESIAN_POINT('Ctrl Pts',(20.7275521347833,-18.2395995564061,
8.26525910813474));
#174687=CARTESIAN_POINT('Ctrl Pts',(20.724611172247,-18.2314226807587,8.26472580091698));
#174688=CARTESIAN_POINT('Ctrl Pts',(20.7200789161847,-18.2190609995525,
8.26392213281046));
#174689=CARTESIAN_POINT('Ctrl Pts',(20.7185245998338,-18.2148628667633,
8.26364965281869));
#174690=CARTESIAN_POINT('Ctrl Pts',(20.7157091024435,-18.2073317975665,
8.26316170322544));
#174691=CARTESIAN_POINT('Ctrl Pts',(20.7144528180605,-18.2039971026539,
8.26294594776046));
#174692=CARTESIAN_POINT('Ctrl Pts',(20.7117028615495,-18.1967530837837,
8.26247792499275));
#174693=CARTESIAN_POINT('Ctrl Pts',(20.7102060208389,-18.1928450244311,
8.26222585052816));
#174694=CARTESIAN_POINT('Ctrl Pts',(20.7059640713711,-18.1818674045298,
8.26151888954884));
#174695=CARTESIAN_POINT('Ctrl Pts',(20.7031925171357,-18.1748080367215,
8.26106556076175));
#174696=CARTESIAN_POINT('Ctrl Pts',(20.6862933924865,-18.1324354155725,
8.25835147320396));
#174697=CARTESIAN_POINT('Ctrl Pts',(20.6712532371401,-18.0974908431281,
8.25614222485884));
#174698=CARTESIAN_POINT('Ctrl Pts',(20.618387017022,-17.9832421357649,8.24895634796574));
#174699=CARTESIAN_POINT('Ctrl Pts',(20.5765656166621,-17.905883073821,8.24414894956654));
#174700=CARTESIAN_POINT('Ctrl Pts',(20.4377981800777,-17.6834835102052,
8.22988831967376));
#174701=CARTESIAN_POINT('Ctrl Pts',(20.3276493221905,-17.5476006951211,
8.22051299753978));
#174702=CARTESIAN_POINT('Ctrl Pts',(20.1854714729081,-17.4107497918513,
8.20904691332124));
#174703=CARTESIAN_POINT('Ctrl Pts',(20.1685835225989,-17.3950184022049,
8.20769489533522));
#174704=CARTESIAN_POINT('Ctrl Pts',(20.1443409473992,-17.3731653609786,
8.20576612629853));
#174705=CARTESIAN_POINT('Ctrl Pts',(20.1371964692755,-17.3668122920801,
8.20519914683374));
#174706=CARTESIAN_POINT('Ctrl Pts',(20.1255216297847,-17.3565714718254,
8.20427485361015));
#174707=CARTESIAN_POINT('Ctrl Pts',(20.1210173752236,-17.3526540604435,
8.20391878111463));
#174708=CARTESIAN_POINT('Ctrl Pts',(20.1115571240338,-17.3444963727913,
8.20317199165996));
#174709=CARTESIAN_POINT('Ctrl Pts',(20.1065979860016,-17.3402598507168,
8.20278112516494));
#174710=CARTESIAN_POINT('Ctrl Pts',(20.0947589921745,-17.3302402331746,
8.2018493971262));
#174711=CARTESIAN_POINT('Ctrl Pts',(20.0878617723182,-17.3244779345155,
8.20130769244963));
#174712=CARTESIAN_POINT('Ctrl Pts',(20.0645262536377,-17.3052332043154,
8.19947848690033));
#174713=CARTESIAN_POINT('Ctrl Pts',(20.0479220171919,-17.2919548584491,
8.19818279334596));
#174714=CARTESIAN_POINT('Ctrl Pts',(19.9114075633507,-17.1861160763221,
8.1875737599483));
#174715=CARTESIAN_POINT('Ctrl Pts',(19.7821003146753,-17.1064365206708,
8.17774705098268));
#174716=CARTESIAN_POINT('Ctrl Pts',(19.5191246388494,-16.9809977040795,
8.15851560158897));
#174717=CARTESIAN_POINT('Ctrl Pts',(19.3871506701713,-16.9334184897505,
8.14919461729016));
#174718=CARTESIAN_POINT('Ctrl Pts',(19.23644457044,-16.8954306371134,8.13950223934659));
#174719=CARTESIAN_POINT('Ctrl Pts',(19.2214095381892,-16.891815526537,8.13854575362525));
#174720=CARTESIAN_POINT('Ctrl Pts',(19.2007251342864,-16.8870811693372,
8.13724545788543));
#174721=CARTESIAN_POINT('Ctrl Pts',(19.1951092245429,-16.8858198498143,
8.13689399154264));
#174722=CARTESIAN_POINT('Ctrl Pts',(19.1861635909178,-16.8838489715824,
8.13633671070011));
#174723=CARTESIAN_POINT('Ctrl Pts',(19.1828372269972,-16.8831245244486,
8.13613005524956));
#174724=CARTESIAN_POINT('Ctrl Pts',(19.1759522425594,-16.8816424335891,
8.13570350426253));
#174725=CARTESIAN_POINT('Ctrl Pts',(19.1723934130695,-16.8808859391544,
8.13548368062842));
#174726=CARTESIAN_POINT('Ctrl Pts',(19.1638900632026,-16.8791012956302,
8.13495998133655));
#174727=CARTESIAN_POINT('Ctrl Pts',(19.1589437408244,-16.8780816497858,
8.13465659087138));
#174728=CARTESIAN_POINT('Ctrl Pts',(19.1421626701402,-16.8746849193374,
8.13363135550849));
#174729=CARTESIAN_POINT('Ctrl Pts',(19.1303110049797,-16.8723913079019,
8.13291411399844));
#174730=CARTESIAN_POINT('Ctrl Pts',(19.1017333270388,-16.86711395191,8.13119965966214));
#174731=CARTESIAN_POINT('Ctrl Pts',(19.0849895158324,-16.8642298904186,
8.13020748512273));
#174732=CARTESIAN_POINT('Ctrl Pts',(19.0217244606241,-16.8541153536498,
8.12649892941144));
#174733=CARTESIAN_POINT('Ctrl Pts',(18.9749985768257,-16.8482353714438,
8.12384163635732));
#174734=CARTESIAN_POINT('Ctrl Pts',(18.7632271502125,-16.8287354086484,
8.11201370457759));
#174735=CARTESIAN_POINT('Ctrl Pts',(18.5971284965,-16.8329489394972,8.10327870512878));
#174736=CARTESIAN_POINT('Ctrl Pts',(18.4027335682835,-16.8608520798403,
8.09232662014656));
#174737=CARTESIAN_POINT('Ctrl Pts',(18.3723551781013,-16.86589118554,8.09059532991768));
#174738=CARTESIAN_POINT('Ctrl Pts',(18.2937323065434,-16.8807019426397,
8.08605037475608));
#174739=CARTESIAN_POINT('Ctrl Pts',(18.2457018107127,-16.8914962726911,
8.08321018944067));
#174740=CARTESIAN_POINT('Ctrl Pts',(18.1858482775165,-16.9071579758446,
8.07957177276679));
#174741=CARTESIAN_POINT('Ctrl Pts',(18.1736321517393,-16.9104718765634,
8.07882394229243));
#174742=CARTESIAN_POINT('Ctrl Pts',(18.1543405001009,-16.915891371491,8.07763438708182));
#174743=CARTESIAN_POINT('Ctrl Pts',(18.1472448854976,-16.9179248007014,
8.07719501152915));
#174744=CARTESIAN_POINT('Ctrl Pts',(18.1340548380325,-16.9217795044507,
8.07637475104678));
#174745=CARTESIAN_POINT('Ctrl Pts',(18.1279576822433,-16.9235912232399,
8.07599418210902));
#174746=CARTESIAN_POINT('Ctrl Pts',(18.1144478245515,-16.9276719144909,
8.07514778032247));
#174747=CARTESIAN_POINT('Ctrl Pts',(18.1070392608751,-16.9299541733713,
8.07468151631386));
#174748=CARTESIAN_POINT('Ctrl Pts',(18.0855918511831,-16.9366903964074,
8.07332548491994));
#174749=CARTESIAN_POINT('Ctrl Pts',(18.0715869542553,-16.9412501733404,
8.07243225241572));
#174750=CARTESIAN_POINT('Ctrl Pts',(17.9873784937238,-16.9696423609099,
8.06701348595055));
#174751=CARTESIAN_POINT('Ctrl Pts',(17.9184263739569,-16.9970005007686,
8.06237164937812));
#174752=CARTESIAN_POINT('Ctrl Pts',(17.7205270314199,-17.0878145250312,
8.04843614210774));
#174753=CARTESIAN_POINT('Ctrl Pts',(17.5964399298002,-17.1608371091457,
8.0388698710998));
#174754=CARTESIAN_POINT('Ctrl Pts',(17.4064916748834,-17.3003667216467,
8.02337001411286));
#174755=CARTESIAN_POINT('Ctrl Pts',(17.3358956587051,-17.3596812259989,
8.01738979410201));
#174756=CARTESIAN_POINT('Ctrl Pts',(17.2623997116989,-17.4301014891053,
8.01110119090848));
#174757=CARTESIAN_POINT('Ctrl Pts',(17.2554640631812,-17.4368386298259,
8.01050712697695));
#174758=CARTESIAN_POINT('Ctrl Pts',(17.2452868616776,-17.4468609749741,
8.00963482222536));
#174759=CARTESIAN_POINT('Ctrl Pts',(17.2420096152402,-17.4501095294314,
8.00935383252509));
#174760=CARTESIAN_POINT('Ctrl Pts',(17.2362121345813,-17.4558939570463,
8.00885664041529));
#174761=CARTESIAN_POINT('Ctrl Pts',(17.2336876790408,-17.4584255218394,
8.00864010483995));
#174762=CARTESIAN_POINT('Ctrl Pts',(17.2282901889713,-17.463865705465,8.00817706177173));
#174763=CARTESIAN_POINT('Ctrl Pts',(17.2254191711242,-17.466776246824,8.00793071165759));
#174764=CARTESIAN_POINT('Ctrl Pts',(17.2195440036225,-17.4727669059542,
8.00742643931674));
#174765=CARTESIAN_POINT('Ctrl Pts',(17.216540774211,-17.4758479040816,8.00716858826537));
#174766=CARTESIAN_POINT('Ctrl Pts',(17.20275671955,-17.49007541738,8.00598462437137));
#174767=CARTESIAN_POINT('Ctrl Pts',(17.1920888537718,-17.5013313549203,
8.00506692452257));
#174768=CARTESIAN_POINT('Ctrl Pts',(17.1269831423748,-17.5715557275963,
7.99944984538999));
#174769=CARTESIAN_POINT('Ctrl Pts',(17.0758055800885,-17.6334691607406,
7.99496142150964));
#174770=CARTESIAN_POINT('Ctrl Pts',(16.9870647272263,-17.7541917324801,
7.98672447870772));
#174771=CARTESIAN_POINT('Ctrl Pts',(16.9486527687872,-17.8122354844151,
7.98296209881663));
#174772=CARTESIAN_POINT('Ctrl Pts',(16.8464128603342,-17.9846179973398,
7.97206948302796));
#174773=CARTESIAN_POINT('Ctrl Pts',(16.7902668398971,-18.1030670588315,
7.96490115903004));
#174774=CARTESIAN_POINT('Ctrl Pts',(16.7454193380512,-18.2258898493182,
7.95734463868439));
#174775=CARTESIAN_POINT('Ctrl Pts',(16.7454193803189,-18.2258897335605,
7.7340522080425));
#174776=CARTESIAN_POINT('Ctrl Pts',(16.7619322267477,-18.1806664005465,
7.73723213666382));
#174777=CARTESIAN_POINT('Ctrl Pts',(16.779998976002,-18.1359755434987,7.74040817555081));
#174778=CARTESIAN_POINT('Ctrl Pts',(16.8255358480881,-18.0335613432304,
7.74771677785878));
#174779=CARTESIAN_POINT('Ctrl Pts',(16.8541026592798,-17.9764219531316,
7.75181782248633));
#174780=CARTESIAN_POINT('Ctrl Pts',(16.8915487563,-17.9092959968522,7.75659240664854));
#174781=CARTESIAN_POINT('Ctrl Pts',(16.8979909436681,-17.8979938387207,
7.75739475456953));
#174782=CARTESIAN_POINT('Ctrl Pts',(16.9071560003972,-17.8822537265884,
7.7585091882223));
#174783=CARTESIAN_POINT('Ctrl Pts',(16.9097915255555,-17.8777656068379,
7.75882661551778));
#174784=CARTESIAN_POINT('Ctrl Pts',(16.9143119584172,-17.8701322280941,
7.75936585096772));
#174785=CARTESIAN_POINT('Ctrl Pts',(16.9161885259259,-17.8669820784768,
7.75958819498853));
#174786=CARTESIAN_POINT('Ctrl Pts',(16.9198038258629,-17.8609488662358,
7.76001364754557));
#174787=CARTESIAN_POINT('Ctrl Pts',(16.9215412559203,-17.8580650676948,
7.76021684147643));
#174788=CARTESIAN_POINT('Ctrl Pts',(16.9261670066246,-17.85042848667,7.76075450913471));
#174789=CARTESIAN_POINT('Ctrl Pts',(16.929067212396,-17.8456828823784,7.76108820995248));
#174790=CARTESIAN_POINT('Ctrl Pts',(16.9394508641136,-17.8288416397558,
7.76227114815962));
#174791=CARTESIAN_POINT('Ctrl Pts',(16.9470376561362,-17.8168097474834,
7.7631138752276));
#174792=CARTESIAN_POINT('Ctrl Pts',(17.0551881142097,-17.649065318899,7.77484241498185));
#174793=CARTESIAN_POINT('Ctrl Pts',(17.1756723125731,-17.5071175146947,
7.78457133713022));
#174794=CARTESIAN_POINT('Ctrl Pts',(17.3915911146781,-17.3116247103171,
7.80052204703916));
#174795=CARTESIAN_POINT('Ctrl Pts',(17.475264179863,-17.2465754267534,7.80642246470033));
#174796=CARTESIAN_POINT('Ctrl Pts',(17.5762508346356,-17.1795604063647,
7.81347122822371));
#174797=CARTESIAN_POINT('Ctrl Pts',(17.5891496151711,-17.1712016337461,
7.81437005807411));
#174798=CARTESIAN_POINT('Ctrl Pts',(17.6099153271888,-17.1580637285884,
7.81581532395711));
#174799=CARTESIAN_POINT('Ctrl Pts',(17.6177245335891,-17.1531940692189,
7.81635844164296));
#174800=CARTESIAN_POINT('Ctrl Pts',(17.6326611028114,-17.1440146562094,
7.81739664682125));
#174801=CARTESIAN_POINT('Ctrl Pts',(17.6397826475457,-17.1396957340488,
7.8178913874317));
#174802=CARTESIAN_POINT('Ctrl Pts',(17.6523561103436,-17.1321715765748,
7.81876450383632));
#174803=CARTESIAN_POINT('Ctrl Pts',(17.6577972825859,-17.1289485184373,
7.8191422230715));
#174804=CARTESIAN_POINT('Ctrl Pts',(17.6684890635192,-17.1226798288853,
7.81988423028138));
#174805=CARTESIAN_POINT('Ctrl Pts',(17.6737384940372,-17.1196323016415,
7.82024844459872));
#174806=CARTESIAN_POINT('Ctrl Pts',(17.6863080467173,-17.1124072171097,
7.82112035062422));
#174807=CARTESIAN_POINT('Ctrl Pts',(17.6936401107291,-17.1082507400902,
7.8216287970201));
#174808=CARTESIAN_POINT('Ctrl Pts',(17.7201258929756,-17.093444492107,7.82346504575633));
#174809=CARTESIAN_POINT('Ctrl Pts',(17.7394193751252,-17.0830487955071,
7.82480188044333));
#174810=CARTESIAN_POINT('Ctrl Pts',(17.9252216831591,-16.9866267596963,
7.83767285470048));
#174811=CARTESIAN_POINT('Ctrl Pts',(18.1022711915946,-16.9227871890543,
7.85002447788917));
#174812=CARTESIAN_POINT('Ctrl Pts',(18.362532564999,-16.8663497467016,7.86760356587159));
#174813=CARTESIAN_POINT('Ctrl Pts',(18.4405888349051,-16.8539445666954,
7.87278915021938));
#174814=CARTESIAN_POINT('Ctrl Pts',(18.5546862687292,-16.8423055161878,
7.88009811166932));
#174815=CARTESIAN_POINT('Ctrl Pts',(18.5903007764088,-16.8395807443077,
7.88234120915035));
#174816=CARTESIAN_POINT('Ctrl Pts',(18.6334065997711,-16.8373781844339,
7.88499652782441));
#174817=CARTESIAN_POINT('Ctrl Pts',(18.6408457924727,-16.8370374111,7.88545263849376));
#174818=CARTESIAN_POINT('Ctrl Pts',(18.6524384052315,-16.8365676633924,
7.88615990157103));
#174819=CARTESIAN_POINT('Ctrl Pts',(18.6565905836826,-16.8364116545375,
7.88641252567698));
#174820=CARTESIAN_POINT('Ctrl Pts',(18.6643073826521,-16.8361444620529,
7.88688069236927));
#174821=CARTESIAN_POINT('Ctrl Pts',(18.6678717904873,-16.8360300619921,
7.88709640717752));
#174822=CARTESIAN_POINT('Ctrl Pts',(18.6759507355909,-16.8357912015704,
7.88758414484032));
#174823=CARTESIAN_POINT('Ctrl Pts',(18.6804653808177,-16.8356721801511,
7.88785586045923));
#174824=CARTESIAN_POINT('Ctrl Pts',(18.6938518795006,-16.8353621298321,
7.88865913214287));
#174825=CARTESIAN_POINT('Ctrl Pts',(18.7027247184456,-16.8352124320093,
7.88918843209379));
#174826=CARTESIAN_POINT('Ctrl Pts',(18.7689738607688,-16.8345113601344,
7.89311886455338));
#174827=CARTESIAN_POINT('Ctrl Pts',(18.8263558471927,-16.8362370289468,
7.89640252499328));
#174828=CARTESIAN_POINT('Ctrl Pts',(18.9373969122156,-16.8441036246973,
7.90264250938221));
#174829=CARTESIAN_POINT('Ctrl Pts',(18.9910290967687,-16.8499690835869,
7.90560438632877));
#174830=CARTESIAN_POINT('Ctrl Pts',(19.1590174935583,-16.874867505714,7.91486773977388));
#174831=CARTESIAN_POINT('Ctrl Pts',(19.272061961036,-16.9012421038396,7.92109154937541));
#174832=CARTESIAN_POINT('Ctrl Pts',(19.4555541449726,-16.9602777650855,
7.93180169213588));
#174833=CARTESIAN_POINT('Ctrl Pts',(19.5273857443055,-16.9877863932878,
7.9361563097903));
#174834=CARTESIAN_POINT('Ctrl Pts',(19.6149542720312,-17.0269099726207,
7.94175497383186));
#174835=CARTESIAN_POINT('Ctrl Pts',(19.6322444966816,-17.0349165818859,
7.94287486320842));
#174836=CARTESIAN_POINT('Ctrl Pts',(19.6571777634614,-17.0468738185945,
7.94451186082426));
#174837=CARTESIAN_POINT('Ctrl Pts',(19.6649088220748,-17.0506395103291,
7.94502256021687));
#174838=CARTESIAN_POINT('Ctrl Pts',(19.6784036865335,-17.0573147066109,
7.94591956771264));
#174839=CARTESIAN_POINT('Ctrl Pts',(19.6841775606311,-17.0602036880333,
7.94630515477249));
#174840=CARTESIAN_POINT('Ctrl Pts',(19.6953492316343,-17.0658575253039,
7.94705474327523));
#174841=CARTESIAN_POINT('Ctrl Pts',(19.7007485461323,-17.0686192558652,
7.94741863198299));
#174842=CARTESIAN_POINT('Ctrl Pts',(19.7136050897967,-17.0752651852286,
7.9482889880279));
#174843=CARTESIAN_POINT('Ctrl Pts',(19.7210511489608,-17.0791706636548,
7.94879620397142));
#174844=CARTESIAN_POINT('Ctrl Pts',(19.7477072312569,-17.0933549755273,
7.95062340435189));
#174845=CARTESIAN_POINT('Ctrl Pts',(19.7667810685412,-17.1038855862021,
7.9519523052246));
#174846=CARTESIAN_POINT('Ctrl Pts',(19.9494190141715,-17.2084298056783,
7.96488992636055));
#174847=CARTESIAN_POINT('Ctrl Pts',(20.0998578013824,-17.3236008205379,
7.97732859494697));
#174848=CARTESIAN_POINT('Ctrl Pts',(20.2882103200328,-17.5124763347102,
7.99493368496722));
#174849=CARTESIAN_POINT('Ctrl Pts',(20.340298153315,-17.5708388955554,8.00006424234782));
#174850=CARTESIAN_POINT('Ctrl Pts',(20.4111709102989,-17.6596973118171,
8.00730621820389));
#174851=CARTESIAN_POINT('Ctrl Pts',(20.4326005973129,-17.6879964974435,
8.00953510571154));
#174852=CARTESIAN_POINT('Ctrl Pts',(20.4576469260583,-17.7228598422889,
8.01217592008974));
#174853=CARTESIAN_POINT('Ctrl Pts',(20.4619521441968,-17.7289196084709,
8.01263118941461));
#174854=CARTESIAN_POINT('Ctrl Pts',(20.4686123393807,-17.7383994594772,
8.01333743474378));
#174855=CARTESIAN_POINT('Ctrl Pts',(20.4709892738495,-17.7418039402209,
8.01358987573566));
#174856=CARTESIAN_POINT('Ctrl Pts',(20.4753893193302,-17.7481457899185,
8.01405787710751));
#174857=CARTESIAN_POINT('Ctrl Pts',(20.4774150039841,-17.7510812497255,
8.01427360862288));
#174858=CARTESIAN_POINT('Ctrl Pts',(20.4819912336812,-17.7577487369091,
8.01476160568835));
#174859=CARTESIAN_POINT('Ctrl Pts',(20.4845372437389,-17.7614838129727,
8.01503356263084));
#174860=CARTESIAN_POINT('Ctrl Pts',(20.4920565838355,-17.7725911940076,
8.01583820945556));
#174861=CARTESIAN_POINT('Ctrl Pts',(20.4969955169397,-17.7799868187015,
8.01636863173673));
#174862=CARTESIAN_POINT('Ctrl Pts',(20.5337421013779,-17.8357695688771,
8.02033127904505));
#174863=CARTESIAN_POINT('Ctrl Pts',(20.5636021136094,-17.8854169582913,
8.02364384496398));
#174864=CARTESIAN_POINT('Ctrl Pts',(20.6709720017695,-18.081748845276,8.03618223822287));
#174865=CARTESIAN_POINT('Ctrl Pts',(20.7331795830118,-18.236119283212,8.04492057814872));
#174866=CARTESIAN_POINT('Ctrl Pts',(20.7976855332202,-18.4731881153562,
8.0585476936874));
#174867=CARTESIAN_POINT('Ctrl Pts',(20.8142664358205,-18.5513151337539,
8.06306155630676));
#174868=CARTESIAN_POINT('Ctrl Pts',(20.8293525981671,-18.6494036783684,
8.06885223255477));
#174869=CARTESIAN_POINT('Ctrl Pts',(20.8320432964963,-18.6686603923205,
8.06999469803572));
#174870=CARTESIAN_POINT('Ctrl Pts',(20.8355497042471,-18.6965533123941,
8.07165871287179));
#174871=CARTESIAN_POINT('Ctrl Pts',(20.8365782324318,-18.7051621124621,
8.07217354827358));
#174872=CARTESIAN_POINT('Ctrl Pts',(20.8382816334519,-18.7202034565729,
8.0730753600271));
#174873=CARTESIAN_POINT('Ctrl Pts',(20.8389799678123,-18.7266332675303,
8.07346159151261));
#174874=CARTESIAN_POINT('Ctrl Pts',(20.8402739886179,-18.7390788215124,
8.07421062968914));
#174875=CARTESIAN_POINT('Ctrl Pts',(20.8408733942546,-18.7450941209619,
8.0745733151487));
#174876=CARTESIAN_POINT('Ctrl Pts',(20.8422377982908,-18.7594076049884,
8.07543791860648));
#174877=CARTESIAN_POINT('Ctrl Pts',(20.8429795748212,-18.767707855188,8.07594056272967));
#174878=CARTESIAN_POINT('Ctrl Pts',(20.845445486719,-18.7972682303203,8.07773530678394));
#174879=CARTESIAN_POINT('Ctrl Pts',(20.8468972533344,-18.8185492280345,
8.07903591663865));
#174880=CARTESIAN_POINT('Ctrl Pts',(20.8582309521455,-19.0321854861355,
8.09218220035401));
#174881=CARTESIAN_POINT('Ctrl Pts',(20.8421358513437,-19.2249821324295,
8.1048984775538));
#174882=CARTESIAN_POINT('Ctrl Pts',(20.7837496616184,-19.4867327030221,
8.12259031213804));
#174883=CARTESIAN_POINT('Ctrl Pts',(20.763331094302,-19.5596426708577,8.12755035236347));
#174884=CARTESIAN_POINT('Ctrl Pts',(20.727886639083,-19.6642609590438,8.13458397055187));
#174885=CARTESIAN_POINT('Ctrl Pts',(20.7159104693788,-19.6969367889989,
8.13676813031065));
#174886=CARTESIAN_POINT('Ctrl Pts',(20.7004201116911,-19.7361782665043,
8.13936322713852));
#174887=CARTESIAN_POINT('Ctrl Pts',(20.6976707559909,-19.7430377836054,
8.13981580567058));
#174888=CARTESIAN_POINT('Ctrl Pts',(20.6933241716792,-19.7537199956716,
8.14051879525213));
#174889=CARTESIAN_POINT('Ctrl Pts',(20.6917515766215,-19.7575525594904,
8.14077064991461));
#174890=CARTESIAN_POINT('Ctrl Pts',(20.6888037283009,-19.7646771264926,
8.14123812476935));
#174891=CARTESIAN_POINT('Ctrl Pts',(20.6874314171975,-19.767970236387,8.14145391261085));
#174892=CARTESIAN_POINT('Ctrl Pts',(20.6842963624851,-19.7754401316373,
8.14194275317121));
#174893=CARTESIAN_POINT('Ctrl Pts',(20.6825285274285,-19.779614723521,8.14221549283492));
#174894=CARTESIAN_POINT('Ctrl Pts',(20.6772288581636,-19.792018329585,8.14302460758111));
#174895=CARTESIAN_POINT('Ctrl Pts',(20.673658155661,-19.8002307674279,8.14355867753926));
#174896=CARTESIAN_POINT('Ctrl Pts',(20.6458890944605,-19.8630058728969,
8.14763024012297));
#174897=CARTESIAN_POINT('Ctrl Pts',(20.6194426832431,-19.9165511277936,
8.15104051929581));
#174898=CARTESIAN_POINT('Ctrl Pts',(20.5139728921885,-20.109127048501,8.16332629922221));
#174899=CARTESIAN_POINT('Ctrl Pts',(20.42154249325,-20.2401974200527,8.17176668649212));
#174900=CARTESIAN_POINT('Ctrl Pts',(20.2747034011892,-20.4051474471537,
8.18399127114817));
#174901=CARTESIAN_POINT('Ctrl Pts',(20.2322291312334,-20.4489011702537,
8.18741377976112));
#174902=CARTESIAN_POINT('Ctrl Pts',(20.1611141954442,-20.516095588868,8.1930302633218));
#174903=CARTESIAN_POINT('Ctrl Pts',(20.1336433628314,-20.5407253230825,
8.19517466091691));
#174904=CARTESIAN_POINT('Ctrl Pts',(20.0970921595499,-20.5718122969972,
8.19800331523234));
#174905=CARTESIAN_POINT('Ctrl Pts',(20.0885838117698,-20.5789341728332,
8.1986600818738));
#174906=CARTESIAN_POINT('Ctrl Pts',(20.0746469565321,-20.5904148430398,
8.19973335037634));
#174907=CARTESIAN_POINT('Ctrl Pts',(20.0692521725673,-20.5948143820369,
8.20014819115289));
#174908=CARTESIAN_POINT('Ctrl Pts',(20.0588299209313,-20.6032286556426,
8.20094851183168));
#174909=CARTESIAN_POINT('Ctrl Pts',(20.0538056516013,-20.6072472423159,
8.20133383029686));
#174910=CARTESIAN_POINT('Ctrl Pts',(20.0422514520509,-20.6164026449629,
8.20221885494527));
#174911=CARTESIAN_POINT('Ctrl Pts',(20.035709475102,-20.6215240236994,8.20271916946415));
#174912=CARTESIAN_POINT('Ctrl Pts',(20.0182311539396,-20.6350417235495,
8.2040538829054));
#174913=CARTESIAN_POINT('Ctrl Pts',(20.007242780248,-20.6433698319372,8.20489095314936));
#174914=CARTESIAN_POINT('Ctrl Pts',(19.9216924994318,-20.7069024207235,
8.21139328751848));
#174915=CARTESIAN_POINT('Ctrl Pts',(19.8436657339346,-20.7572517580322,
8.21724511602407));
#174916=CARTESIAN_POINT('Ctrl Pts',(19.6063279225209,-20.8891886399429,
8.23479889722253));
#174917=CARTESIAN_POINT('Ctrl Pts',(19.4396987615087,-20.9559057976099,
8.24688040733223));
#174918=CARTESIAN_POINT('Ctrl Pts',(19.2273849944582,-21.0111037886464,
8.26091880600298));
#174919=CARTESIAN_POINT('Ctrl Pts',(19.1878047697689,-21.0201873452203,
8.2634771630064));
#174920=CARTESIAN_POINT('Ctrl Pts',(19.1404107505338,-21.0296378297155,
8.26645193086106));
#174921=CARTESIAN_POINT('Ctrl Pts',(19.1328282038753,-21.0311067114566,
8.26692517995119));
#174922=CARTESIAN_POINT('Ctrl Pts',(19.1210952105125,-21.033313062624,8.26765314845265));
#174923=CARTESIAN_POINT('Ctrl Pts',(19.1169504064292,-21.0340796703251,
8.26790947909269));
#174924=CARTESIAN_POINT('Ctrl Pts',(19.1092994189575,-21.0354711491618,
8.26838107640478));
#174925=CARTESIAN_POINT('Ctrl Pts',(19.105793974438,-21.0360995475655,8.2685965370917));
#174926=CARTESIAN_POINT('Ctrl Pts',(19.0979157755039,-21.0374913116965,
8.26907940641547));
#174927=CARTESIAN_POINT('Ctrl Pts',(19.0935422101888,-21.0382497699798,
8.26934653398458));
#174928=CARTESIAN_POINT('Ctrl Pts',(19.0823622400183,-21.0401523854795,
8.27002706491561));
#174929=CARTESIAN_POINT('Ctrl Pts',(19.0755525064793,-21.0412770336968,
8.27043938622134));
#174930=CARTESIAN_POINT('Ctrl Pts',(19.0360540379946,-21.0476020481865,
8.27281891744481));
#174931=CARTESIAN_POINT('Ctrl Pts',(19.0032504759751,-21.0520688180703,
8.27474734115056));
#174932=CARTESIAN_POINT('Ctrl Pts',(18.9517122908287,-21.0578590279552,
8.27772129711128));
#174933=CARTESIAN_POINT('Ctrl Pts',(18.9330433891822,-21.0597055426208,
8.27878715527497));
#174934=CARTESIAN_POINT('Ctrl Pts',(18.8831924885211,-21.0639679471237,
8.28160859935259));
#174935=CARTESIAN_POINT('Ctrl Pts',(18.8519767947686,-21.0659414875312,
8.28334967659106));
#174936=CARTESIAN_POINT('Ctrl Pts',(18.7822691807166,-21.0687996229342,
8.28720198555414));
#174937=CARTESIAN_POINT('Ctrl Pts',(18.7437737750249,-21.069327362334,8.28930524138088));
#174938=CARTESIAN_POINT('Ctrl Pts',(18.5960095125387,-21.067322877649,8.29735057932324));
#174939=CARTESIAN_POINT('Ctrl Pts',(18.4870143111089,-21.0573810651917,
8.30323550843215));
#174940=CARTESIAN_POINT('Ctrl Pts',(18.3250240604673,-21.0298489412745,
8.31237249618763));
#174941=CARTESIAN_POINT('Ctrl Pts',(18.2711534090569,-21.0185163759503,
8.31547580097375));
#174942=CARTESIAN_POINT('Ctrl Pts',(18.1845501275153,-20.9967416549042,
8.32061346158843));
#174943=CARTESIAN_POINT('Ctrl Pts',(18.1515215739635,-20.9875791030728,
8.32260855716529));
#174944=CARTESIAN_POINT('Ctrl Pts',(18.1083928115484,-20.9744790211142,
8.32526689862377));
#174945=CARTESIAN_POINT('Ctrl Pts',(18.0980786827963,-20.9712597200122,
8.32590666819378));
#174946=CARTESIAN_POINT('Ctrl Pts',(18.0812216952832,-20.9658562653355,
8.32695908473673));
#174947=CARTESIAN_POINT('Ctrl Pts',(18.0746639870634,-20.963718815554,8.32737019209324));
#174948=CARTESIAN_POINT('Ctrl Pts',(18.0619874506889,-20.9595183259161,
8.32816823083397));
#174949=CARTESIAN_POINT('Ctrl Pts',(18.055867379102,-20.9574592597113,8.3285550272166));
#174950=CARTESIAN_POINT('Ctrl Pts',(18.0417538772452,-20.9526388541996,
8.32945056231596));
#174951=CARTESIAN_POINT('Ctrl Pts',(18.0337674219762,-20.9498575657025,
8.32995995788408));
#174952=CARTESIAN_POINT('Ctrl Pts',(18.0123241681034,-20.9422455659553,
8.33133486694411));
#174953=CARTESIAN_POINT('Ctrl Pts',(17.9988994683721,-20.937326323758,8.33220331248653));
#174954=CARTESIAN_POINT('Ctrl Pts',(17.875670993979,-20.8907502251318,8.34024723497498));
#174955=CARTESIAN_POINT('Ctrl Pts',(17.7694797713999,-20.8401668164009,
8.34772770467395));
#174956=CARTESIAN_POINT('Ctrl Pts',(17.5265483616413,-20.6985881747918,
8.36609795142342));
#174957=CARTESIAN_POINT('Ctrl Pts',(17.3951035307402,-20.5999885505734,
8.37712897988476));
#174958=CARTESIAN_POINT('Ctrl Pts',(17.2538230692569,-20.4658458363614,
8.38949101534657));
#174959=CARTESIAN_POINT('Ctrl Pts',(17.2317792058561,-20.4439738215517,
8.39143495164522));
#174960=CARTESIAN_POINT('Ctrl Pts',(17.2052685503269,-20.4164862902024,
8.39378276540116));
#174961=CARTESIAN_POINT('Ctrl Pts',(17.2003398384282,-20.4113239707356,
8.39421969402791));
#174962=CARTESIAN_POINT('Ctrl Pts',(17.1926298699967,-20.403166367725,8.39490372547208));
#174963=CARTESIAN_POINT('Ctrl Pts',(17.1898310722684,-20.4001878427069,
8.39515215021537));
#174964=CARTESIAN_POINT('Ctrl Pts',(17.1846001212378,-20.3945885757427,
8.39561663827477));
#174965=CARTESIAN_POINT('Ctrl Pts',(17.1821660092802,-20.3919698082353,
8.39583284861467));
#174966=CARTESIAN_POINT('Ctrl Pts',(17.1766043151379,-20.3859557140663,
8.3963270476929));
#174967=CARTESIAN_POINT('Ctrl Pts',(17.1734812015023,-20.3825563217124,
8.39660469554475));
#174968=CARTESIAN_POINT('Ctrl Pts',(17.1638449846068,-20.3719985524893,
8.3974618864648));
#174969=CARTESIAN_POINT('Ctrl Pts',(17.1573697245677,-20.3648055931578,
8.39803863741119));
#174970=CARTESIAN_POINT('Ctrl Pts',(17.0888253090605,-20.2876057486507,
8.4041550904539));
#174971=CARTESIAN_POINT('Ctrl Pts',(17.0314046716022,-20.2135926837676,
8.40937985811453));
#174972=CARTESIAN_POINT('Ctrl Pts',(16.9052198204781,-20.0265625621903,
8.42175707351962));
#174973=CARTESIAN_POINT('Ctrl Pts',(16.8417777048939,-19.9104449575379,
8.42880642808041));
#174974=CARTESIAN_POINT('Ctrl Pts',(16.7672717970289,-19.7373961120652,
8.43927195262707));
#174975=CARTESIAN_POINT('Ctrl Pts',(16.7470574651501,-19.6847520432532,
8.4424477018452));
#174976=CARTESIAN_POINT('Ctrl Pts',(16.7177768297081,-19.5983354043262,
8.44769447256432));
#174977=CARTESIAN_POINT('Ctrl Pts',(16.7074032721517,-19.5650341130707,
8.4497240100253));
#174978=CARTESIAN_POINT('Ctrl Pts',(16.6948809048811,-19.5210347555933,
8.45242171395637));
#174979=CARTESIAN_POINT('Ctrl Pts',(16.6919850793017,-19.510553752222,8.45306550738155));
#174980=CARTESIAN_POINT('Ctrl Pts',(16.6873806765225,-19.4933742939246,
8.45412285755148));
#174981=CARTESIAN_POINT('Ctrl Pts',(16.6856239146994,-19.4866888747486,
8.45453484623635));
#174982=CARTESIAN_POINT('Ctrl Pts',(16.6822909630589,-19.4737476841383,
8.45533339730518));
#174983=CARTESIAN_POINT('Ctrl Pts',(16.680710562815,-19.4674930687072,8.45571981833572));
#174984=CARTESIAN_POINT('Ctrl Pts',(16.6771333681844,-19.4530584379528,
8.45661274639762));
#174985=CARTESIAN_POINT('Ctrl Pts',(16.6751567490611,-19.4448735782977,
8.45711989825493));
#174986=CARTESIAN_POINT('Ctrl Pts',(16.6699846634008,-19.4228826879038,
8.45848483774115));
#174987=CARTESIAN_POINT('Ctrl Pts',(16.6668789476151,-19.4090561835746,
8.45934549164943));
#174988=CARTESIAN_POINT('Ctrl Pts',(16.6325818105127,-19.2488618864125,
8.46934706920211));
#174989=CARTESIAN_POINT('Ctrl Pts',(16.6168624934317,-19.0996426934776,
8.47899859255897));
#174990=CARTESIAN_POINT('Ctrl Pts',(16.6171394762141,-18.8002697688707,
8.49872815360886));
#174991=CARTESIAN_POINT('Ctrl Pts',(16.6331712122105,-18.6509266940689,
8.50874331107301));
#174992=CARTESIAN_POINT('Ctrl Pts',(16.6681544975829,-18.4891628821534,
8.51906805533745));
#174993=CARTESIAN_POINT('Ctrl Pts',(16.6716463807226,-18.4738437285133,
8.52004014730388));
#174994=CARTESIAN_POINT('Ctrl Pts',(16.6766589553073,-18.4529304758363,
8.52135811576691));
#174995=CARTESIAN_POINT('Ctrl Pts',(16.6780324478155,-18.4473020801462,
8.52171191459495));
#174996=CARTESIAN_POINT('Ctrl Pts',(16.6802514660228,-18.4383682263632,
8.52227197272355));
#174997=CARTESIAN_POINT('Ctrl Pts',(16.6810818949191,-18.435059100171,8.52247908773211));
#174998=CARTESIAN_POINT('Ctrl Pts',(16.682813267587,-18.4282298294263,8.52290581785142));
#174999=CARTESIAN_POINT('Ctrl Pts',(16.6837152749943,-18.4247099950044,
8.52312536430036));
#175000=CARTESIAN_POINT('Ctrl Pts',(16.6858857791515,-18.416329981778,8.5236471584064));
#175001=CARTESIAN_POINT('Ctrl Pts',(16.6871625295355,-18.4114719241799,
8.52394893028115));
#175002=CARTESIAN_POINT('Ctrl Pts',(16.6915249191276,-18.3951100642402,
8.52496299762822));
#175003=CARTESIAN_POINT('Ctrl Pts',(16.6946904095671,-18.3836275291725,
8.52567082472598));
#175004=CARTESIAN_POINT('Ctrl Pts',(16.7120038283707,-18.3228320159641,
8.52940108849747));
#175005=CARTESIAN_POINT('Ctrl Pts',(16.727837983075,-18.2740394767152,8.53233405453527));
#175006=CARTESIAN_POINT('Ctrl Pts',(16.74541940036,-18.2258896786745,8.53521106622902));
#175007=CARTESIAN_POINT('Origin',(18.734,-18.952,0.));
#175008=CARTESIAN_POINT('',(16.7437494325541,-18.2252642451362,9.55561791118868));
#175009=CARTESIAN_POINT('',(16.7454193880554,-18.2258897123729,9.33206801777758));
#175010=CARTESIAN_POINT('',(16.7454193692319,-18.2258897639242,0.));
#175011=CARTESIAN_POINT('',(16.6163525130807,-18.950106484017,9.51094372097752));
#175012=CARTESIAN_POINT('Ctrl Pts',(16.6163525130807,-18.950106484017,9.51094372097752));
#175013=CARTESIAN_POINT('Ctrl Pts',(16.6150298054201,-18.8071177642836,
9.51955279572483));
#175014=CARTESIAN_POINT('Ctrl Pts',(16.6379357302198,-18.5602068930662,
9.53444419246188));
#175015=CARTESIAN_POINT('Ctrl Pts',(16.7071052757493,-18.3228113044306,
9.54933558919893));
#175016=CARTESIAN_POINT('Ctrl Pts',(16.7437494325541,-18.2252642451362,
9.55561791118868));
#175017=CARTESIAN_POINT('Ctrl Pts',(16.6170008641637,-18.9500871830904,
9.51057060101912));
#175018=CARTESIAN_POINT('Ctrl Pts',(16.6168630285762,-19.1026359284247,
9.50227624137429));
#175019=CARTESIAN_POINT('Ctrl Pts',(16.6332131376109,-19.2547442788604,
9.49405436693276));
#175020=CARTESIAN_POINT('Ctrl Pts',(16.6711097710214,-19.4282348466107,
9.4838681377401));
#175021=CARTESIAN_POINT('Ctrl Pts',(16.6768854893957,-19.4525951877099,
9.48241989998714));
#175022=CARTESIAN_POINT('Ctrl Pts',(16.6863088548723,-19.4894182436269,
9.48020049124768));
#175023=CARTESIAN_POINT('Ctrl Pts',(16.6896415039904,-19.5019597468797,
9.47943921501431));
#175024=CARTESIAN_POINT('Ctrl Pts',(16.6960379446959,-19.5251691160293,
9.47801999813407));
#175025=CARTESIAN_POINT('Ctrl Pts',(16.6990707475128,-19.5358451033516,
9.4773630695322));
#175026=CARTESIAN_POINT('Ctrl Pts',(16.7041423648668,-19.5531783841545,
9.4762896021547));
#175027=CARTESIAN_POINT('Ctrl Pts',(16.7061303467709,-19.5598504225682,
9.47587472563739));
#175028=CARTESIAN_POINT('Ctrl Pts',(16.7100186725365,-19.5726689746564,
9.47507438167625));
#175029=CARTESIAN_POINT('Ctrl Pts',(16.7119141981425,-19.5788168779883,
9.47468907591658));
#175030=CARTESIAN_POINT('Ctrl Pts',(16.7163213512743,-19.5928828868289,
9.47380414513183));
#175031=CARTESIAN_POINT('Ctrl Pts',(16.7188516072731,-19.6007950033501,
9.47330391220546));
#175032=CARTESIAN_POINT('Ctrl Pts',(16.7257038508009,-19.621795156383,9.47196955823238));
#175033=CARTESIAN_POINT('Ctrl Pts',(16.7301071476363,-19.6348560584379,
9.47113276814319));
#175034=CARTESIAN_POINT('Ctrl Pts',(16.7650760746778,-19.7353278097386,
9.46464131649608));
#175035=CARTESIAN_POINT('Ctrl Pts',(16.801215612779,-19.8206796802427,9.45880081225721));
#175036=CARTESIAN_POINT('Ctrl Pts',(16.8638223093732,-19.9451305581103,
9.44979592761911));
#175037=CARTESIAN_POINT('Ctrl Pts',(16.8861995929533,-19.986169343978,9.44674237297692));
#175038=CARTESIAN_POINT('Ctrl Pts',(16.9361603738986,-20.0709887023405,
9.44027008730656));
#175039=CARTESIAN_POINT('Ctrl Pts',(16.9640285347178,-20.1145678142593,
9.43684913489017));
#175040=CARTESIAN_POINT('Ctrl Pts',(17.0413692551478,-20.226273322753,9.42787444805212));
#175041=CARTESIAN_POINT('Ctrl Pts',(17.0933610523225,-20.2925510143061,
9.4223349661178));
#175042=CARTESIAN_POINT('Ctrl Pts',(17.1737192473799,-20.3832877870346,
9.41460144864412));
#175043=CARTESIAN_POINT('Ctrl Pts',(17.1989999424321,-20.4103675689605,
9.41227279420793));
#175044=CARTESIAN_POINT('Ctrl Pts',(17.2302741118558,-20.4421524866696,
9.40952892294982));
#175045=CARTESIAN_POINT('Ctrl Pts',(17.2355971505706,-20.4475048929915,
9.40906649769853));
#175046=CARTESIAN_POINT('Ctrl Pts',(17.2439142735717,-20.455778914969,9.40835124419744));
#175047=CARTESIAN_POINT('Ctrl Pts',(17.2468885184086,-20.4587202591152,
9.40809689566886));
#175048=CARTESIAN_POINT('Ctrl Pts',(17.2524127758881,-20.464151115818,9.40762715223498));
#175049=CARTESIAN_POINT('Ctrl Pts',(17.2549603344813,-20.4666429836246,
9.4074115749229));
#175050=CARTESIAN_POINT('Ctrl Pts',(17.2607240770139,-20.4722523199491,
9.40692618985666));
#175051=CARTESIAN_POINT('Ctrl Pts',(17.2639438602511,-20.4753660126167,
9.40665667679774));
#175052=CARTESIAN_POINT('Ctrl Pts',(17.2734472413167,-20.4844980725033,
9.40586590515163));
#175053=CARTESIAN_POINT('Ctrl Pts',(17.2797581754032,-20.4904880320007,
9.4053467995836));
#175054=CARTESIAN_POINT('Ctrl Pts',(17.3247712329339,-20.5326872613134,
9.40168516972385));
#175055=CARTESIAN_POINT('Ctrl Pts',(17.3647876100627,-20.5674740385254,
9.39864270924847));
#175056=CARTESIAN_POINT('Ctrl Pts',(17.4206664686786,-20.6124804292018,
9.39460645865098));
#175057=CARTESIAN_POINT('Ctrl Pts',(17.4354176666934,-20.6240419171314,
9.39355996207498));
#175058=CARTESIAN_POINT('Ctrl Pts',(17.6009950400266,-20.7503027312398,
9.38199931053239));
#175059=CARTESIAN_POINT('Ctrl Pts',(17.7664088634658,-20.8444495644443,
9.3720574552812));
#175060=CARTESIAN_POINT('Ctrl Pts',(17.9920076087095,-20.9354380281162,
9.35827608787552));
#175061=CARTESIAN_POINT('Ctrl Pts',(18.0426094513431,-20.9536387080224,
9.3551786841135));
#175062=CARTESIAN_POINT('Ctrl Pts',(18.1058854203258,-20.9737122951147,
9.35127380574584));
#175063=CARTESIAN_POINT('Ctrl Pts',(18.1179583581891,-20.9774237123538,
9.35052740289039));
#175064=CARTESIAN_POINT('Ctrl Pts',(18.1370610730952,-20.9831096032239,
9.34934396473204));
#175065=CARTESIAN_POINT('Ctrl Pts',(18.1440692141918,-20.9851561594403,
9.34890929003115));
#175066=CARTESIAN_POINT('Ctrl Pts',(18.1572084480777,-20.9889194981888,
9.34809332630986));
#175067=CARTESIAN_POINT('Ctrl Pts',(18.1633369862294,-20.9906449567822,
9.34771232532133));
#175068=CARTESIAN_POINT('Ctrl Pts',(18.1770446299411,-20.9944376199626,
9.34685918695421));
#175069=CARTESIAN_POINT('Ctrl Pts',(18.1846276176632,-20.9964903273447,
9.34638658425659));
#175070=CARTESIAN_POINT('Ctrl Pts',(18.203823792604,-21.0015722065065,9.34518847903388));
#175071=CARTESIAN_POINT('Ctrl Pts',(18.2154515255211,-21.0045448864476,
9.34446116041709));
#175072=CARTESIAN_POINT('Ctrl Pts',(18.2810967571627,-21.0207339612208,
9.34034559922399));
#175073=CARTESIAN_POINT('Ctrl Pts',(18.3355890743815,-21.0319157143376,
9.33689253613938));
#175074=CARTESIAN_POINT('Ctrl Pts',(18.4150613046443,-21.0449856603688,
9.33180051495979));
#175075=CARTESIAN_POINT('Ctrl Pts',(18.4397368265098,-21.0485972379414,
9.33021189789655));
#175076=CARTESIAN_POINT('Ctrl Pts',(18.6245329149065,-21.0723179789876,
9.31826188679705));
#175077=CARTESIAN_POINT('Ctrl Pts',(18.7864149674423,-21.0744926401331,
9.30744168130844));
#175078=CARTESIAN_POINT('Ctrl Pts',(18.995687590613,-21.0533349845132,9.29371561837982));
#175079=CARTESIAN_POINT('Ctrl Pts',(19.0442476776019,-21.0467162397084,
9.29055402263721));
#175080=CARTESIAN_POINT('Ctrl Pts',(19.1184180868714,-21.0339705402854,
9.28580165823864));
#175081=CARTESIAN_POINT('Ctrl Pts',(19.1442153128678,-21.0290416798979,
9.284163221157));
#175082=CARTESIAN_POINT('Ctrl Pts',(19.1765304713502,-21.0222418886843,
9.28213469462177));
#175083=CARTESIAN_POINT('Ctrl Pts',(19.1831388721314,-21.0208182549778,
9.28172112802435));
#175084=CARTESIAN_POINT('Ctrl Pts',(19.1936500341221,-21.018501118757,9.28106545813052));
#175085=CARTESIAN_POINT('Ctrl Pts',(19.1975572104995,-21.0176281710175,
9.28082220625388));
#175086=CARTESIAN_POINT('Ctrl Pts',(19.2049662109763,-21.0159507594879,
9.2803618654251));
#175087=CARTESIAN_POINT('Ctrl Pts',(19.208468419012,-21.0151484747797,9.28014466145809));
#175088=CARTESIAN_POINT('Ctrl Pts',(19.2165293682955,-21.0132802638661,
9.27964562006103));
#175089=CARTESIAN_POINT('Ctrl Pts',(19.2210866263909,-21.0122081294922,
9.2793641423444));
#175090=CARTESIAN_POINT('Ctrl Pts',(19.2332997661203,-21.0092920927271,
9.27861146892223));
#175091=CARTESIAN_POINT('Ctrl Pts',(19.2409490626484,-21.0074205563547,
9.27814181724887));
#175092=CARTESIAN_POINT('Ctrl Pts',(19.2983816324014,-20.9930285366406,
9.2746276045876));
#175093=CARTESIAN_POINT('Ctrl Pts',(19.3477095205682,-20.9787426223841,
9.27167729450712));
#175094=CARTESIAN_POINT('Ctrl Pts',(19.4099602963827,-20.958232370704,9.26798503429809));
#175095=CARTESIAN_POINT('Ctrl Pts',(19.4234025416554,-20.9536530159695,
9.267189625697));
#175096=CARTESIAN_POINT('Ctrl Pts',(19.57171929182,-20.9014547674071,9.25842426669654));
#175097=CARTESIAN_POINT('Ctrl Pts',(19.7014852396573,-20.840418299427,9.25083035381799));
#175098=CARTESIAN_POINT('Ctrl Pts',(19.9038114445807,-20.7188827754983,
9.23783216521445));
#175099=CARTESIAN_POINT('Ctrl Pts',(19.980264472034,-20.6658131544802,9.23261206732595));
#175100=CARTESIAN_POINT('Ctrl Pts',(20.0694824216427,-20.5947479920948,
9.22596826874101));
#175101=CARTESIAN_POINT('Ctrl Pts',(20.0857896716596,-20.5813553633962,
9.22472985428435));
#175102=CARTESIAN_POINT('Ctrl Pts',(20.1087323899523,-20.5619317213766,
9.22295150285492));
#175103=CARTESIAN_POINT('Ctrl Pts',(20.1155342873075,-20.5560985944487,
9.22241965478348));
#175104=CARTESIAN_POINT('Ctrl Pts',(20.1272192451607,-20.5459484348279,
9.22149787738007));
#175105=CARTESIAN_POINT('Ctrl Pts',(20.1321198142782,-20.5416516792789,
9.22110879221236));
#175106=CARTESIAN_POINT('Ctrl Pts',(20.1414750085189,-20.5333724430294,
9.22036117783167));
#175107=CARTESIAN_POINT('Ctrl Pts',(20.1459327734786,-20.5293935923596,
9.22000280286259));
#175108=CARTESIAN_POINT('Ctrl Pts',(20.1575026569676,-20.5189783644121,
9.21906703842031));
#175109=CARTESIAN_POINT('Ctrl Pts',(20.1645879218864,-20.5125124805477,
9.21848840416575));
#175110=CARTESIAN_POINT('Ctrl Pts',(20.1887103820941,-20.4901964097252,
9.21649896808299));
#175111=CARTESIAN_POINT('Ctrl Pts',(20.2055295826899,-20.4741140266492,
9.21507825397089));
#175112=CARTESIAN_POINT('Ctrl Pts',(20.3440141903878,-20.3372553014399,
9.20309082120404));
#175113=CARTESIAN_POINT('Ctrl Pts',(20.4508381515618,-20.2024090510055,
9.19185658233501));
#175114=CARTESIAN_POINT('Ctrl Pts',(20.5871043900858,-19.979507910268,9.17459271599519));
#175115=CARTESIAN_POINT('Ctrl Pts',(20.6290584778028,-19.8999049204125,
9.1686615346981));
#175116=CARTESIAN_POINT('Ctrl Pts',(20.6815904813275,-19.7827019421545,
9.16045637286842));
#175117=CARTESIAN_POINT('Ctrl Pts',(20.6963918647558,-19.7471056538739,
9.15803089502281));
#175118=CARTESIAN_POINT('Ctrl Pts',(20.7129436603057,-19.7040165795312,
9.15519024427024));
#175119=CARTESIAN_POINT('Ctrl Pts',(20.7156349976042,-19.6968957557035,
9.15472387953935));
#175120=CARTESIAN_POINT('Ctrl Pts',(20.7197484629079,-19.6858321380763,
9.15400422203568));
#175121=CARTESIAN_POINT('Ctrl Pts',(20.7211973585329,-19.6818994614036,
9.15374937473223));
#175122=CARTESIAN_POINT('Ctrl Pts',(20.7238564117507,-19.6746154964506,
9.1532791688215));
#175123=CARTESIAN_POINT('Ctrl Pts',(20.7250697775859,-19.671265483801,9.15306362487697));
#175124=CARTESIAN_POINT('Ctrl Pts',(20.727785886357,-19.6637069679382,9.1525788911479));
#175125=CARTESIAN_POINT('Ctrl Pts',(20.7292837607456,-19.6594967729928,
9.15230999255343));
#175126=CARTESIAN_POINT('Ctrl Pts',(20.7336428087024,-19.6471204985923,
9.15152269194647));
#175127=CARTESIAN_POINT('Ctrl Pts',(20.7364673011132,-19.6389414703811,
9.15100641474822));
#175128=CARTESIAN_POINT('Ctrl Pts',(20.7558475575602,-19.5816856739003,
9.14741883653966));
#175129=CARTESIAN_POINT('Ctrl Pts',(20.7706489808566,-19.532028847478,9.14444304396547));
#175130=CARTESIAN_POINT('Ctrl Pts',(20.7889953217657,-19.4610631632442,
9.14031546702329));
#175131=CARTESIAN_POINT('Ctrl Pts',(20.7940584928292,-19.4401701816199,
9.13911537110776));
#175132=CARTESIAN_POINT('Ctrl Pts',(20.8292194241577,-19.2847765979516,
9.13027778356622));
#175133=CARTESIAN_POINT('Ctrl Pts',(20.8464368504934,-19.1476985621164,
9.12294755883473));
#175134=CARTESIAN_POINT('Ctrl Pts',(20.8526907917146,-18.9191824569172,
9.11034420747673));
#175135=CARTESIAN_POINT('Ctrl Pts',(20.8493359723429,-18.8283931623072,
9.10524188335007));
#175136=CARTESIAN_POINT('Ctrl Pts',(20.8380618689454,-18.7173797977746,
9.09874057585315));
#175137=CARTESIAN_POINT('Ctrl Pts',(20.8356512825713,-18.6966868032178,
9.09751771301583));
#175138=CARTESIAN_POINT('Ctrl Pts',(20.8317736991271,-18.6671948462735,
9.09575784127902));
#175139=CARTESIAN_POINT('Ctrl Pts',(20.8305558260603,-18.6583639449104,
9.09522868979839));
#175140=CARTESIAN_POINT('Ctrl Pts',(20.8283522355628,-18.6430985848412,
9.09431009661379));
#175141=CARTESIAN_POINT('Ctrl Pts',(20.8273925425078,-18.6366604490288,
9.093921483184));
#175142=CARTESIAN_POINT('Ctrl Pts',(20.825493449877,-18.6243111649564,9.09317372452792));
#175143=CARTESIAN_POINT('Ctrl Pts',(20.8245586428585,-18.6183993658331,
9.09281472849929));
#175144=CARTESIAN_POINT('Ctrl Pts',(20.8220516560144,-18.6029694160947,
9.09187500465252));
#175145=CARTESIAN_POINT('Ctrl Pts',(20.8204394760468,-18.5934579875939,
9.09129301129374));
#175146=CARTESIAN_POINT('Ctrl Pts',(20.8146594297214,-18.5607170936752,
9.08928005889486));
#175147=CARTESIAN_POINT('Ctrl Pts',(20.8101682864919,-18.537547167095,9.08783887014091));
#175148=CARTESIAN_POINT('Ctrl Pts',(20.7711450461931,-18.3528141391553,
9.0762103655146));
#175149=CARTESIAN_POINT('Ctrl Pts',(20.718200834135,-18.1957520440936,9.06540857010438));
#175150=CARTESIAN_POINT('Ctrl Pts',(20.5930548615233,-17.9312940756027,
9.04607406590476));
#175151=CARTESIAN_POINT('Ctrl Pts',(20.5282575334772,-17.8212603286336,
9.03764638292147));
#175152=CARTESIAN_POINT('Ctrl Pts',(20.4469596082138,-17.7079734169417,
9.02899834211065));
#175153=CARTESIAN_POINT('Ctrl Pts',(20.4398862330722,-17.6982915275852,
9.02825963610064));
#175154=CARTESIAN_POINT('Ctrl Pts',(20.429725237027,-17.6846285915678,9.02721834955958));
#175155=CARTESIAN_POINT('Ctrl Pts',(20.4267052287265,-17.6805978699693,
9.02691130383708));
#175156=CARTESIAN_POINT('Ctrl Pts',(20.4214803304768,-17.6736759589614,
9.02638432512594));
#175157=CARTESIAN_POINT('Ctrl Pts',(20.4192823334509,-17.6707796142039,
9.02616391457937));
#175158=CARTESIAN_POINT('Ctrl Pts',(20.4150096533626,-17.6651794376228,
9.02573794579844));
#175159=CARTESIAN_POINT('Ctrl Pts',(20.4129359031929,-17.6624749526261,
9.02553232236138));
#175160=CARTESIAN_POINT('Ctrl Pts',(20.4073307929739,-17.6552014794134,
9.0249795211916));
#175161=CARTESIAN_POINT('Ctrl Pts',(20.4037872245758,-17.65064187399,9.02463319910274));
#175162=CARTESIAN_POINT('Ctrl Pts',(20.3906101320906,-17.6338289890199,
9.02335676117982));
#175163=CARTESIAN_POINT('Ctrl Pts',(20.3808597597506,-17.6216673695781,
9.02243458343505));
#175164=CARTESIAN_POINT('Ctrl Pts',(20.2843001082529,-17.5039174710135,
9.01350486822727));
#175165=CARTESIAN_POINT('Ctrl Pts',(20.1875786924896,-17.4068486173566,
9.00612142620185));
#175166=CARTESIAN_POINT('Ctrl Pts',(19.9630196291148,-17.2213707213965,
8.99030483061929));
#175167=CARTESIAN_POINT('Ctrl Pts',(19.8334806452871,-17.1363178140282,
8.98188544487261));
#175168=CARTESIAN_POINT('Ctrl Pts',(19.6768994420232,-17.0564573188982,
8.97164904727588));
#175169=CARTESIAN_POINT('Ctrl Pts',(19.6578075229907,-17.0470797849851,
8.97040087663036));
#175170=CARTESIAN_POINT('Ctrl Pts',(19.6304507516507,-17.0341507211708,
8.96861094213637));
#175171=CARTESIAN_POINT('Ctrl Pts',(19.6222991734192,-17.030361537347,8.96807741411682));
#175172=CARTESIAN_POINT('Ctrl Pts',(19.6081915301588,-17.0239126798679,
8.96715364965005));
#175173=CARTESIAN_POINT('Ctrl Pts',(19.6022468072357,-17.0212283859265,
8.96676426729695));
#175174=CARTESIAN_POINT('Ctrl Pts',(19.590838302584,-17.0161403063087,8.96601672877439));
#175175=CARTESIAN_POINT('Ctrl Pts',(19.5853765656866,-17.0137320689082,
8.96565872996057));
#175176=CARTESIAN_POINT('Ctrl Pts',(19.5711423429917,-17.007527561138,8.96472537405398));
#175177=CARTESIAN_POINT('Ctrl Pts',(19.562354273364,-17.0037675803344,8.96414878476424));
#175178=CARTESIAN_POINT('Ctrl Pts',(19.5322725828297,-16.9911374403592,
8.96217376390338));
#175179=CARTESIAN_POINT('Ctrl Pts',(19.5108601772163,-16.9825560954173,
8.96076561271371));
#175180=CARTESIAN_POINT('Ctrl Pts',(19.3263064449611,-16.9120713856958,
8.94860481902744));
#175181=CARTESIAN_POINT('Ctrl Pts',(19.1562579689345,-16.8702193128321,
8.93715752021208));
#175182=CARTESIAN_POINT('Ctrl Pts',(18.8959421133494,-16.839381431829,8.91983712807145));
#175183=CARTESIAN_POINT('Ctrl Pts',(18.8082760399015,-16.8344855449401,
8.9140546311083));
#175184=CARTESIAN_POINT('Ctrl Pts',(18.6825554808543,-16.835284044295,8.90602655449178));
#175185=CARTESIAN_POINT('Ctrl Pts',(18.6445671301375,-16.8365484754125,
8.90363599244644));
#175186=CARTESIAN_POINT('Ctrl Pts',(18.5990627640118,-16.8392912112434,
8.90083070727008));
#175187=CARTESIAN_POINT('Ctrl Pts',(18.5914970681917,-16.8397880309577,
8.90036623056498));
#175188=CARTESIAN_POINT('Ctrl Pts',(18.5797601669503,-16.8406221126032,
8.89964885381658));
#175189=CARTESIAN_POINT('Ctrl Pts',(18.5755871061486,-16.8409311083605,
8.89939441463954));
#175190=CARTESIAN_POINT('Ctrl Pts',(18.5678619268868,-16.841526157585,8.8989245873623));
#175191=CARTESIAN_POINT('Ctrl Pts',(18.5643096450214,-16.8418088042587,
8.89870901632222));
#175192=CARTESIAN_POINT('Ctrl Pts',(18.5562959080279,-16.8424668051246,
8.89822375057582));
#175193=CARTESIAN_POINT('Ctrl Pts',(18.5518349327411,-16.842847342248,8.89795434992376));
#175194=CARTESIAN_POINT('Ctrl Pts',(18.5387170287545,-16.8440082753117,
8.89716421376405));
#175195=CARTESIAN_POINT('Ctrl Pts',(18.5300635393934,-16.8448278484872,
8.89664562609733));
#175196=CARTESIAN_POINT('Ctrl Pts',(18.4689435004876,-16.8509965790054,
8.89299995147784));
#175197=CARTESIAN_POINT('Ctrl Pts',(18.4166832583751,-16.8582518305724,
8.8899719299562));
#175198=CARTESIAN_POINT('Ctrl Pts',(18.3492009418416,-16.8702056154985,
8.8861158071719));
#175199=CARTESIAN_POINT('Ctrl Pts',(18.3336886604828,-16.8731327547037,
8.88523314299887));
#175200=CARTESIAN_POINT('Ctrl Pts',(18.2683583034559,-16.8862188532635,
8.88152637930244));
#175201=CARTESIAN_POINT('Ctrl Pts',(18.218880467618,-16.8979975289314,8.87874487286666));
#175202=CARTESIAN_POINT('Ctrl Pts',(18.0644204496828,-16.9407012860923,
8.87001964490624));
#175203=CARTESIAN_POINT('Ctrl Pts',(17.9613874506527,-16.9779867623235,
8.86412866468287));
#175204=CARTESIAN_POINT('Ctrl Pts',(17.8114225671373,-17.0458035634928,
8.8549776090888));
#175205=CARTESIAN_POINT('Ctrl Pts',(17.7620546639081,-17.0704964548709,
8.85186624081543));
#175206=CARTESIAN_POINT('Ctrl Pts',(17.6836215447672,-17.1136384126272,
8.84671642245495));
#175207=CARTESIAN_POINT('Ctrl Pts',(17.6539415351062,-17.1309174262474,
8.8447174767515));
#175208=CARTESIAN_POINT('Ctrl Pts',(17.615486751019,-17.1545757249732,8.84205473274584));
#175209=CARTESIAN_POINT('Ctrl Pts',(17.6063211130725,-17.160311903814,8.84141451012977));
#175210=CARTESIAN_POINT('Ctrl Pts',(17.5913800238297,-17.1698226277735,
8.84036153816167));
#175211=CARTESIAN_POINT('Ctrl Pts',(17.5855782989727,-17.1735556823739,
8.83995033161849));
#175212=CARTESIAN_POINT('Ctrl Pts',(17.5743824824523,-17.1808371335567,
8.83915223598762));
#175213=CARTESIAN_POINT('Ctrl Pts',(17.5689861668501,-17.1843819831173,
8.83876548261964));
#175214=CARTESIAN_POINT('Ctrl Pts',(17.5565627275212,-17.1926245659259,
8.83787024469848));
#175215=CARTESIAN_POINT('Ctrl Pts',(17.5495473900773,-17.1973397878062,
8.83736110466524));
#175216=CARTESIAN_POINT('Ctrl Pts',(17.5307542226738,-17.210135307839,8.83598733247383));
#175217=CARTESIAN_POINT('Ctrl Pts',(17.5190297758388,-17.2182928894541,
8.83511977580285));
#175218=CARTESIAN_POINT('Ctrl Pts',(17.3924219239212,-17.3082985312384,
8.82563479820473));
#175219=CARTESIAN_POINT('Ctrl Pts',(17.2859326239898,-17.4012989398142,
8.8165676813664));
#175220=CARTESIAN_POINT('Ctrl Pts',(17.1234054325967,-17.5746791701776,
8.80093330374722));
#175221=CARTESIAN_POINT('Ctrl Pts',(17.0622207663085,-17.649624508218,8.79450513321501));
#175222=CARTESIAN_POINT('Ctrl Pts',(16.9686660987399,-17.7817260525203,
8.78394199412348));
#175223=CARTESIAN_POINT('Ctrl Pts',(16.9334397144459,-17.836684264969,8.77974786839756));
#175224=CARTESIAN_POINT('Ctrl Pts',(16.8942250415197,-17.9045792667621,
8.77487642530745));
#175225=CARTESIAN_POINT('Ctrl Pts',(16.8877510578125,-17.9160333240194,
8.77406483650845));
#175226=CARTESIAN_POINT('Ctrl Pts',(16.8788540525536,-17.9321226307659,
8.77293983791907));
#175227=CARTESIAN_POINT('Ctrl Pts',(16.8763409389655,-17.936707357999,8.77262095320507));
#175228=CARTESIAN_POINT('Ctrl Pts',(16.8720920953019,-17.9445272052275,
8.7720799852235));
#175229=CARTESIAN_POINT('Ctrl Pts',(16.8703477576582,-17.947757599918,8.77185735784182));
#175230=CARTESIAN_POINT('Ctrl Pts',(16.8670223269083,-17.9539545761097,
8.77143192836215));
#175231=CARTESIAN_POINT('Ctrl Pts',(16.8654398911356,-17.9569203951959,
8.77122903816278));
#175232=CARTESIAN_POINT('Ctrl Pts',(16.8612708339721,-17.9647791020992,
8.77069328874368));
#175233=CARTESIAN_POINT('Ctrl Pts',(16.858696303531,-17.9696784242801,8.77036119213161));
#175234=CARTESIAN_POINT('Ctrl Pts',(16.8496512053957,-17.9870563738762,
8.76918976646572));
#175235=CARTESIAN_POINT('Ctrl Pts',(16.8432855757738,-17.999589599478,8.76835678229432));
#175236=CARTESIAN_POINT('Ctrl Pts',(16.8025847915486,-18.0817415215493,
8.76296777001828));
#175237=CARTESIAN_POINT('Ctrl Pts',(16.7720027305155,-18.1530865146677,
8.75861677565704));
#175238=CARTESIAN_POINT('Ctrl Pts',(16.7454192490578,-18.2258900930424,
8.75434673926218));
#175239=CARTESIAN_POINT('',(16.6170000979997,-18.9526441512856,9.29097292592683));
#175240=CARTESIAN_POINT('Ctrl Pts',(16.74541940036,-18.2258896786745,8.53521106622902));
#175241=CARTESIAN_POINT('Ctrl Pts',(16.7707333810102,-18.1565628982361,
8.53935342956444));
#175242=CARTESIAN_POINT('Ctrl Pts',(16.7996695249671,-18.0885686098479,
8.54338075134243));
#175243=CARTESIAN_POINT('Ctrl Pts',(16.9057914982917,-17.8715014022299,
8.55651366874445));
#175244=CARTESIAN_POINT('Ctrl Pts',(16.9970988704475,-17.7301198635963,
8.56556714094202));
#175245=CARTESIAN_POINT('Ctrl Pts',(17.1191104689661,-17.5829229396598,
8.57667155906595));
#175246=CARTESIAN_POINT('Ctrl Pts',(17.1343922610984,-17.5650987016149,
8.578046558463));
#175247=CARTESIAN_POINT('Ctrl Pts',(17.1563534137942,-17.5403297407529,
8.58000255525429));
#175248=CARTESIAN_POINT('Ctrl Pts',(17.1627889134241,-17.5331704159487,
8.58057339835522));
#175249=CARTESIAN_POINT('Ctrl Pts',(17.173301900474,-17.5216342353551,8.58150227676022));
#175250=CARTESIAN_POINT('Ctrl Pts',(17.1773495487018,-17.5172302798447,
8.58185904591863));
#175251=CARTESIAN_POINT('Ctrl Pts',(17.1858429074168,-17.5080675130306,
8.58260591182747));
#175252=CARTESIAN_POINT('Ctrl Pts',(17.190292015493,-17.5033119496111,8.58299615200241));
#175253=CARTESIAN_POINT('Ctrl Pts',(17.2008948677985,-17.4920830758555,
8.58392385028291));
#175254=CARTESIAN_POINT('Ctrl Pts',(17.2070677385546,-17.4856280700579,
8.58446213218822));
#175255=CARTESIAN_POINT('Ctrl Pts',(17.2278430921896,-17.4641765920693,
8.58626788552569));
#175256=CARTESIAN_POINT('Ctrl Pts',(17.2426267496613,-17.4493580257008,
8.58754326629444));
#175257=CARTESIAN_POINT('Ctrl Pts',(17.3232616703567,-17.3708949518692,
8.5944509953967));
#175258=CARTESIAN_POINT('Ctrl Pts',(17.3929624790881,-17.3113628103603,
8.6002576527638));
#175259=CARTESIAN_POINT('Ctrl Pts',(17.5419206457441,-17.199985842425,8.61232139718495));
#175260=CARTESIAN_POINT('Ctrl Pts',(17.6212468292611,-17.1485628769628,
8.61857368246792));
#175261=CARTESIAN_POINT('Ctrl Pts',(17.768585038123,-17.0664832176997,8.62971089495122));
#175262=CARTESIAN_POINT('Ctrl Pts',(17.8352936647747,-17.0337904807951,
8.63459302445037));
#175263=CARTESIAN_POINT('Ctrl Pts',(17.9424467806769,-16.9880963998862,
8.64206172811646));
#175264=CARTESIAN_POINT('Ctrl Pts',(17.9817987943188,-16.9726900828249,
8.64472884211933));
#175265=CARTESIAN_POINT('Ctrl Pts',(18.0286043463917,-16.9559635570945,
8.64779172826197));
#175266=CARTESIAN_POINT('Ctrl Pts',(18.0356335873788,-16.9534933407631,
8.64824884770175));
#175267=CARTESIAN_POINT('Ctrl Pts',(18.0470291418705,-16.9495561796841,
8.64898511912869));
#175268=CARTESIAN_POINT('Ctrl Pts',(18.0513873874885,-16.9480663095785,
8.6492655770485));
#175269=CARTESIAN_POINT('Ctrl Pts',(18.0591363508056,-16.9454455327002,
8.64976218236681));
#175270=CARTESIAN_POINT('Ctrl Pts',(18.0625251001908,-16.9443089792394,
8.64997865998579));
#175271=CARTESIAN_POINT('Ctrl Pts',(18.0698013086391,-16.9418890933881,
8.65044197204889));
#175272=CARTESIAN_POINT('Ctrl Pts',(18.0736896053204,-16.9406084563625,
8.65068864705649));
#175273=CARTESIAN_POINT('Ctrl Pts',(18.0843955128988,-16.9371167830364,
8.65136539024046));
#175274=CARTESIAN_POINT('Ctrl Pts',(18.0912207481571,-16.9349290532042,
8.65179410762295));
#175275=CARTESIAN_POINT('Ctrl Pts',(18.1280704624381,-16.9233234487379,
8.65409478999922));
#175276=CARTESIAN_POINT('Ctrl Pts',(18.158292699233,-16.9145406761252,8.65593179343324));
#175277=CARTESIAN_POINT('Ctrl Pts',(18.3467774069107,-16.8642951730654,
8.66714516335542));
#175278=CARTESIAN_POINT('Ctrl Pts',(18.5092219737297,-16.8406165988855,
8.67579049982962));
#175279=CARTESIAN_POINT('Ctrl Pts',(18.7898605169018,-16.8324985983528,
8.69115899577846));
#175280=CARTESIAN_POINT('Ctrl Pts',(18.9069971206828,-16.8388333486223,
8.69769646010416));
#175281=CARTESIAN_POINT('Ctrl Pts',(19.037160292252,-16.8567703830268,8.70539387941988));
#175282=CARTESIAN_POINT('Ctrl Pts',(19.0512998106917,-16.8588650005664,
8.70623560963288));
#175283=CARTESIAN_POINT('Ctrl Pts',(19.0737683371549,-16.8624263645663,
8.70758247870083));
#175284=CARTESIAN_POINT('Ctrl Pts',(19.08211179315,-16.863800134772,8.70808467435583));
#175285=CARTESIAN_POINT('Ctrl Pts',(19.0968115300974,-16.8663110283114,
8.70897316252749));
#175286=CARTESIAN_POINT('Ctrl Pts',(19.1031712938407,-16.8674273225974,
8.70935878865232));
#175287=CARTESIAN_POINT('Ctrl Pts',(19.1163141391513,-16.8697962449153,
8.71015828837228));
#175288=CARTESIAN_POINT('Ctrl Pts',(19.1230963970159,-16.8710529630091,
8.71057228813985));
#175289=CARTESIAN_POINT('Ctrl Pts',(19.1404885970841,-16.8743636484169,
8.71163765078004));
#175290=CARTESIAN_POINT('Ctrl Pts',(19.1510890762332,-16.8764657351217,
8.71229054233705));
#175291=CARTESIAN_POINT('Ctrl Pts',(19.1952560089527,-16.8855761059651,
8.71502597897021));
#175292=CARTESIAN_POINT('Ctrl Pts',(19.2286642496198,-16.8933179264966,
8.71713184207863));
#175293=CARTESIAN_POINT('Ctrl Pts',(19.3152006939139,-16.9155993350422,
8.7226861181525));
#175294=CARTESIAN_POINT('Ctrl Pts',(19.3679729758349,-16.9314061859861,
8.72617291309199));
#175295=CARTESIAN_POINT('Ctrl Pts',(19.5235311801617,-16.9846945198407,
8.73674189068159));
#175296=CARTESIAN_POINT('Ctrl Pts',(19.6240874574687,-17.0281000056727,
8.74397246603521));
#175297=CARTESIAN_POINT('Ctrl Pts',(19.7612298217737,-17.1003593926661,
8.75421234953124));
#175298=CARTESIAN_POINT('Ctrl Pts',(19.8009293096326,-17.1229466699482,
8.75722311688506));
#175299=CARTESIAN_POINT('Ctrl Pts',(19.859354122805,-17.1587378044619,8.76169856617015));
#175300=CARTESIAN_POINT('Ctrl Pts',(19.8786461373539,-17.1709900403236,
8.76318389400198));
#175301=CARTESIAN_POINT('Ctrl Pts',(19.8983381788674,-17.1839484950669,
8.76470522952686));
#175302=CARTESIAN_POINT('Ctrl Pts',(19.8989397027039,-17.1843447711925,
8.76475170612455));
#175303=CARTESIAN_POINT('Ctrl Pts',(19.9093196853547,-17.1911905691447,
8.76555379886705));
#175304=CARTESIAN_POINT('Ctrl Pts',(19.9190448152208,-17.1977209430552,
8.7663066054662));
#175305=CARTESIAN_POINT('Ctrl Pts',(19.9615332160783,-17.2267662429557,
8.76959978061649));
#175306=CARTESIAN_POINT('Ctrl Pts',(19.993715118187,-17.2501223306543,8.77210533928319));
#175307=CARTESIAN_POINT('Ctrl Pts',(20.0310198149775,-17.2788347001436,
8.77500533300245));
#175308=CARTESIAN_POINT('Ctrl Pts',(20.036794194504,-17.2833269309374,8.77545408978137));
#175309=CARTESIAN_POINT('Ctrl Pts',(20.0461338900775,-17.2906708648774,
8.77617954991592));
#175310=CARTESIAN_POINT('Ctrl Pts',(20.0497134163073,-17.2935042816611,
8.77645749887072));
#175311=CARTESIAN_POINT('Ctrl Pts',(20.056076061162,-17.2985742726507,8.77695135128344));
#175312=CARTESIAN_POINT('Ctrl Pts',(20.0588627078105,-17.3008063246679,
8.7771675710494));
#175313=CARTESIAN_POINT('Ctrl Pts',(20.0648532866858,-17.3056295957145,
8.77763222374122));
#175314=CARTESIAN_POINT('Ctrl Pts',(20.0680552947937,-17.3082231143224,
8.77788048725601));
#175315=CARTESIAN_POINT('Ctrl Pts',(20.0769004824201,-17.3154302872363,
8.77856608325657));
#175316=CARTESIAN_POINT('Ctrl Pts',(20.0825274994277,-17.320063813374,8.7790020056961));
#175317=CARTESIAN_POINT('Ctrl Pts',(20.1136815796057,-17.3459885821679,
8.78141492372732));
#175318=CARTESIAN_POINT('Ctrl Pts',(20.1387298970722,-17.367850976131,8.78335279928629));
#175319=CARTESIAN_POINT('Ctrl Pts',(20.2828303393658,-17.4997300914263,
8.79455974396646));
#175320=CARTESIAN_POINT('Ctrl Pts',(20.3894542881583,-17.6225467322782,
8.80312847868512));
#175321=CARTESIAN_POINT('Ctrl Pts',(20.5468989136072,-17.8525951960539,
8.81839057546747));
#175322=CARTESIAN_POINT('Ctrl Pts',(20.6046989046002,-17.9541153572129,
8.82490257014341));
#175323=CARTESIAN_POINT('Ctrl Pts',(20.6598629322717,-18.0728270393192,
8.83257131875202));
#175324=CARTESIAN_POINT('Ctrl Pts',(20.6657523681689,-18.0858441815338,
8.83341267923289));
#175325=CARTESIAN_POINT('Ctrl Pts',(20.6749161555204,-18.106656905823,8.8347590671924));
#175326=CARTESIAN_POINT('Ctrl Pts',(20.678276408377,-18.1144143540516,8.83526115479853));
#175327=CARTESIAN_POINT('Ctrl Pts',(20.6841209298184,-18.1281316560446,
8.83614951711061));
#175328=CARTESIAN_POINT('Ctrl Pts',(20.6866245797609,-18.1340831716026,
8.83653512603061));
#175329=CARTESIAN_POINT('Ctrl Pts',(20.6917467853633,-18.1464169109117,
8.8373346542141));
#175330=CARTESIAN_POINT('Ctrl Pts',(20.6943614467336,-18.152800659764,8.83774869996632));
#175331=CARTESIAN_POINT('Ctrl Pts',(20.7009932277821,-18.1692206539178,
8.83881431603844));
#175332=CARTESIAN_POINT('Ctrl Pts',(20.7049647226067,-18.1792750047753,
8.83946741644684));
#175333=CARTESIAN_POINT('Ctrl Pts',(20.7212225845643,-18.2213747510842,
8.84220487724658));
#175334=CARTESIAN_POINT('Ctrl Pts',(20.7328052184087,-18.2536846434152,
8.84431259885345));
#175335=CARTESIAN_POINT('Ctrl Pts',(20.7609362091929,-18.3386006516564,
8.84987294595921));
#175336=CARTESIAN_POINT('Ctrl Pts',(20.7762227953239,-18.3915944426824,
8.85336405812305));
#175337=CARTESIAN_POINT('Ctrl Pts',(20.815622075701,-18.5513607421501,8.86394132841973));
#175338=CARTESIAN_POINT('Ctrl Pts',(20.8335432536107,-18.6594646310493,
8.8711758515804));
#175339=CARTESIAN_POINT('Ctrl Pts',(20.8474060880404,-18.8187596475218,
8.8817381523845));
#175340=CARTESIAN_POINT('Ctrl Pts',(20.8499827578842,-18.8692018768008,
8.88506646946332));
#175341=CARTESIAN_POINT('Ctrl Pts',(20.8509990984719,-18.9357845838867,
8.88940640514325));
#175342=CARTESIAN_POINT('Ctrl Pts',(20.8510612007608,-18.9518825741748,
8.89045153783671));
#175343=CARTESIAN_POINT('Ctrl Pts',(20.8505408594561,-19.0208144810576,
8.89490519603126));
#175344=CARTESIAN_POINT('Ctrl Pts',(20.8481641613965,-19.0736205240313,
8.89826291639159));
#175345=CARTESIAN_POINT('Ctrl Pts',(20.8430977553295,-19.1349514952874,
8.90205897609979));
#175346=CARTESIAN_POINT('Ctrl Pts',(20.8423285908031,-19.1436119785177,
8.90259258713674));
#175347=CARTESIAN_POINT('Ctrl Pts',(20.8410824960576,-19.156725191264,8.90339662131618));
#175348=CARTESIAN_POINT('Ctrl Pts',(20.8406447683038,-19.161181428815,8.90366916639451));
#175349=CARTESIAN_POINT('Ctrl Pts',(20.8398332862593,-19.1691816506499,
8.90415718533631));
#175350=CARTESIAN_POINT('Ctrl Pts',(20.8394647209433,-19.1727260934717,
8.9043729454267));
#175351=CARTESIAN_POINT('Ctrl Pts',(20.8386439520309,-19.1804301673681,
8.90484092401625));
#175352=CARTESIAN_POINT('Ctrl Pts',(20.8381883677766,-19.1845893802244,
8.90509294997138));
#175353=CARTESIAN_POINT('Ctrl Pts',(20.8368727698817,-19.1962796960497,
8.90579963787527));
#175354=CARTESIAN_POINT('Ctrl Pts',(20.8359846249692,-19.2038076578319,
8.90625274402571));
#175355=CARTESIAN_POINT('Ctrl Pts',(20.8304050277208,-19.2490126464546,
8.90896267933825));
#175356=CARTESIAN_POINT('Ctrl Pts',(20.8247407956105,-19.2865652127778,
8.91116818116476));
#175357=CARTESIAN_POINT('Ctrl Pts',(20.8026809969307,-19.4101690270752,
8.91833568787673));
#175358=CARTESIAN_POINT('Ctrl Pts',(20.7819557481995,-19.49535955668,8.92312944802086));
#175359=CARTESIAN_POINT('Ctrl Pts',(20.7042810264226,-19.7458418592295,
8.9373967861409));
#175360=CARTESIAN_POINT('Ctrl Pts',(20.6321156280594,-19.9055945393919,
8.94679033544867));
#175361=CARTESIAN_POINT('Ctrl Pts',(20.5291478701635,-20.0743478175533,
8.9582769002772));
#175362=CARTESIAN_POINT('Ctrl Pts',(20.5168194381478,-20.0938297985582,
8.95962749100166));
#175363=CARTESIAN_POINT('Ctrl Pts',(20.4989341961079,-20.1210969210556,
8.96155457079823));
#175364=CARTESIAN_POINT('Ctrl Pts',(20.493638762524,-20.1290521434007,8.96212131182955));
#175365=CARTESIAN_POINT('Ctrl Pts',(20.484948766516,-20.1419172420257,8.96304532225663));
#175366=CARTESIAN_POINT('Ctrl Pts',(20.4815869445198,-20.1468491520082,
8.96340135191915));
#175367=CARTESIAN_POINT('Ctrl Pts',(20.4745075487481,-20.1571410799231,
8.96414813773317));
#175368=CARTESIAN_POINT('Ctrl Pts',(20.4707859734524,-20.1624982572097,
8.96453904380131));
#175369=CARTESIAN_POINT('Ctrl Pts',(20.4618759675462,-20.1751984630982,
8.96547102512627));
#175370=CARTESIAN_POINT('Ctrl Pts',(20.4566654305012,-20.1825257616187,
8.96601294473323));
#175371=CARTESIAN_POINT('Ctrl Pts',(20.4389654320089,-20.2070835629081,
8.96784363054389));
#175372=CARTESIAN_POINT('Ctrl Pts',(20.4262631924642,-20.2241584452287,
8.96914060749162));
#175373=CARTESIAN_POINT('Ctrl Pts',(20.316513208859,-20.3671361899699,8.98021090387019));
#175374=CARTESIAN_POINT('Ctrl Pts',(20.2058436204575,-20.4819074450298,
8.99055444421387));
#175375=CARTESIAN_POINT('Ctrl Pts',(19.9816860549938,-20.667341056288,9.00977090472789));
#175376=CARTESIAN_POINT('Ctrl Pts',(19.8723136670722,-20.7417942748256,
9.01853740067588));
#175377=CARTESIAN_POINT('Ctrl Pts',(19.7428964467634,-20.8132001163442,
9.02775916370466));
#175378=CARTESIAN_POINT('Ctrl Pts',(19.7289973681852,-20.8206674890089,
9.02873539691066));
#175379=CARTESIAN_POINT('Ctrl Pts',(19.7098729082994,-20.8306683440707,
9.03005805370258));
#175380=CARTESIAN_POINT('Ctrl Pts',(19.7047190655604,-20.8333365402677,
9.03041247088327));
#175381=CARTESIAN_POINT('Ctrl Pts',(19.6965163204595,-20.8375405023389,
9.03097326549515));
#175382=CARTESIAN_POINT('Ctrl Pts',(19.6934746079729,-20.8390901224238,
9.03118050256191));
#175383=CARTESIAN_POINT('Ctrl Pts',(19.6871886278916,-20.842273428251,9.03160728263267));
#175384=CARTESIAN_POINT('Ctrl Pts',(19.6839439025983,-20.8439061223958,
9.03182675782657));
#175385=CARTESIAN_POINT('Ctrl Pts',(19.6762085905846,-20.8477734913775,
9.03234805716762));
#175386=CARTESIAN_POINT('Ctrl Pts',(19.6717141986754,-20.8500005905063,
9.03264940797466));
#175387=CARTESIAN_POINT('Ctrl Pts',(19.6565584903362,-20.8574437016793,
9.03366058426841));
#175388=CARTESIAN_POINT('Ctrl Pts',(19.6458610133971,-20.8625861339258,
9.03436597598689));
#175389=CARTESIAN_POINT('Ctrl Pts',(19.5216139043341,-20.9210322495935,
9.04246922492686));
#175390=CARTESIAN_POINT('Ctrl Pts',(19.403569002682,-20.9642400456941,9.04931465220911));
#175391=CARTESIAN_POINT('Ctrl Pts',(19.1205901345057,-21.0401319521696,
9.06523873236093));
#175392=CARTESIAN_POINT('Ctrl Pts',(18.954245119642,-21.064162901218,9.07428093662903));
#175393=CARTESIAN_POINT('Ctrl Pts',(18.763330926184,-21.0689271218655,9.08537263647293));
#175394=CARTESIAN_POINT('Ctrl Pts',(18.7398416394232,-21.0691222338113,
9.08674830842891));
#175395=CARTESIAN_POINT('Ctrl Pts',(18.7067264063761,-21.0688462061143,
9.08870510288752));
#175396=CARTESIAN_POINT('Ctrl Pts',(18.6970989597298,-21.0687002664106,
9.08927605979562));
#175397=CARTESIAN_POINT('Ctrl Pts',(18.6814925356846,-21.0683571884216,
9.09020507335883));
#175398=CARTESIAN_POINT('Ctrl Pts',(18.6755127405624,-21.0682003738174,
9.09056186313289));
#175399=CARTESIAN_POINT('Ctrl Pts',(18.6630247316007,-21.0678199161917,
9.09130873184955));
#175400=CARTESIAN_POINT('Ctrl Pts',(18.6565167329074,-21.0675915835359,
9.09169895403839));
#175401=CARTESIAN_POINT('Ctrl Pts',(18.6410870944815,-21.0669789442939,
9.09262653584781));
#175402=CARTESIAN_POINT('Ctrl Pts',(18.63216668178,-21.0665682098953,9.09316471870992));
#175403=CARTESIAN_POINT('Ctrl Pts',(18.6023559332431,-21.0650065234067,
9.09496979662281));
#175404=CARTESIAN_POINT('Ctrl Pts',(18.5814806166089,-21.0636023576063,
9.09624459292769));
#175405=CARTESIAN_POINT('Ctrl Pts',(18.4694354938249,-21.0543955936917,
9.10314691339842));
#175406=CARTESIAN_POINT('Ctrl Pts',(18.3788344572455,-21.0409986283336,
9.10894844110241));
#175407=CARTESIAN_POINT('Ctrl Pts',(18.1531878048994,-20.9925279187472,
9.12391743573088));
#175408=CARTESIAN_POINT('Ctrl Pts',(18.0202131521194,-20.9498993305473,
9.13323938819729));
#175409=CARTESIAN_POINT('Ctrl Pts',(17.8281654951898,-20.8666938525714,
9.14689238567651));
#175410=CARTESIAN_POINT('Ctrl Pts',(17.7653491741727,-20.8356948704209,
9.15138499664787));
#175411=CARTESIAN_POINT('Ctrl Pts',(17.6959956719678,-20.7970809552874,
9.15628648949651));
#175412=CARTESIAN_POINT('Ctrl Pts',(17.6878429362671,-20.7924706251381,
9.15686170508571));
#175413=CARTESIAN_POINT('Ctrl Pts',(17.6757709390881,-20.7855378377513,
9.15771168739144));
#175414=CARTESIAN_POINT('Ctrl Pts',(17.671828271653,-20.7832566636659,9.15798900771693));
#175415=CARTESIAN_POINT('Ctrl Pts',(17.6649129401629,-20.7792256993459,
9.15847488380465));
#175416=CARTESIAN_POINT('Ctrl Pts',(17.6619371654353,-20.7774813549325,
9.15868378663543));
#175417=CARTESIAN_POINT('Ctrl Pts',(17.6555274277038,-20.7737030052578,
9.1591333667015));
#175418=CARTESIAN_POINT('Ctrl Pts',(17.652094958916,-20.7716665659519,9.15937388243075));
#175419=CARTESIAN_POINT('Ctrl Pts',(17.6450113625614,-20.7674368312581,
9.15986978594795));
#175420=CARTESIAN_POINT('Ctrl Pts',(17.6413610502791,-20.7652421975629,
9.16012508641768));
#175421=CARTESIAN_POINT('Ctrl Pts',(17.6321699391551,-20.759678502172,9.1607673446987));
#175422=CARTESIAN_POINT('Ctrl Pts',(17.6266379070732,-20.7562949447757,
9.16115339571808));
#175423=CARTESIAN_POINT('Ctrl Pts',(17.6108813636068,-20.7465580042894,
9.16225173783336));
#175424=CARTESIAN_POINT('Ctrl Pts',(17.6006952046886,-20.740142655728,9.16296030543165));
#175425=CARTESIAN_POINT('Ctrl Pts',(17.5664517758317,-20.7181656271403,
9.16533926958006));
#175426=CARTESIAN_POINT('Ctrl Pts',(17.542654945412,-20.702201987201,9.1669873235692));
#175427=CARTESIAN_POINT('Ctrl Pts',(17.4296327733063,-20.6230095455563,
9.17482668618842));
#175428=CARTESIAN_POINT('Ctrl Pts',(17.3450663812284,-20.5534099958714,
9.18073558902244));
#175429=CARTESIAN_POINT('Ctrl Pts',(17.1610092087018,-20.3763303474538,
9.19460722556702));
#175430=CARTESIAN_POINT('Ctrl Pts',(17.0665396363283,-20.2644733542615,
9.20257816518851));
#175431=CARTESIAN_POINT('Ctrl Pts',(16.9708097368195,-20.1239327853639,
9.21244913664345));
#175432=CARTESIAN_POINT('Ctrl Pts',(16.9576222347561,-20.1038456161284,
9.21385587400786));
#175433=CARTESIAN_POINT('Ctrl Pts',(16.9395851049211,-20.0753248156304,
9.2158495496874));
#175434=CARTESIAN_POINT('Ctrl Pts',(16.9344470335754,-20.0670751424633,
9.21642579402243));
#175435=CARTESIAN_POINT('Ctrl Pts',(16.9262299301674,-20.0536770655229,
9.21736109271528));
#175436=CARTESIAN_POINT('Ctrl Pts',(16.9231156186708,-20.0485503811497,
9.21771884587233));
#175437=CARTESIAN_POINT('Ctrl Pts',(16.9166725990919,-20.03784177286,9.21846587846381));
#175438=CARTESIAN_POINT('Ctrl Pts',(16.9133477267191,-20.0322576248815,
9.21885529296861));
#175439=CARTESIAN_POINT('Ctrl Pts',(16.9055529058073,-20.019027955422,9.21977759822382));
#175440=CARTESIAN_POINT('Ctrl Pts',(16.9011051428366,-20.0113695638317,
9.22031128696624));
#175441=CARTESIAN_POINT('Ctrl Pts',(16.8865236913145,-19.9858957240665,
9.22208590464507));
#175442=CARTESIAN_POINT('Ctrl Pts',(16.8766009171385,-19.9679614559711,
9.22333437484109));
#175443=CARTESIAN_POINT('Ctrl Pts',(16.8254384926348,-19.8722358350156,
9.22999540829818));
#175444=CARTESIAN_POINT('Ctrl Pts',(16.7888263458494,-19.7920815953588,
9.2355686450241));
#175445=CARTESIAN_POINT('Ctrl Pts',(16.6888399781642,-19.5313024798964,
9.25364997506636));
#175446=CARTESIAN_POINT('Ctrl Pts',(16.6448890658211,-19.3442761693131,
9.2666242487563));
#175447=CARTESIAN_POINT('Ctrl Pts',(16.6241532271979,-19.1278429736965,
9.28035986942869));
#175448=CARTESIAN_POINT('Ctrl Pts',(16.6221401954527,-19.1017413330554,
9.2819938706623));
#175449=CARTESIAN_POINT('Ctrl Pts',(16.6202046990401,-19.0686491058861,
9.28403145854135));
#175450=CARTESIAN_POINT('Ctrl Pts',(16.6198320670926,-19.0616883897599,
9.28445814625456));
#175451=CARTESIAN_POINT('Ctrl Pts',(16.6192953239925,-19.0506400838953,
9.28513224348439));
#175452=CARTESIAN_POINT('Ctrl Pts',(16.6191086720229,-19.0465537116183,
9.28538088288105));
#175453=CARTESIAN_POINT('Ctrl Pts',(16.6187836663981,-19.0389552499614,
9.28584191301783));
#175454=CARTESIAN_POINT('Ctrl Pts',(16.6186422162471,-19.0354433961295,
9.28605446952001));
#175455=CARTESIAN_POINT('Ctrl Pts',(16.6183781735518,-19.0284551322572,
9.28647641291076));
#175456=CARTESIAN_POINT('Ctrl Pts',(16.6182554037863,-19.0249787899557,
9.28668580824344));
#175457=CARTESIAN_POINT('Ctrl Pts',(16.6179937476281,-19.017013171257,9.28716449377872));
#175458=CARTESIAN_POINT('Ctrl Pts',(16.6178605777674,-19.0125237062291,
9.28743346964533));
#175459=CARTESIAN_POINT('Ctrl Pts',(16.6175253051032,-18.9998612865493,
9.28818989902979));
#175460=CARTESIAN_POINT('Ctrl Pts',(16.6173562536645,-18.991687437871,9.28867559344325));
#175461=CARTESIAN_POINT('Ctrl Pts',(16.617081385903,-18.9732240527242,9.28976724482838));
#175462=CARTESIAN_POINT('Ctrl Pts',(16.6170032290319,-18.9629342723496,
9.29037180646726));
#175463=CARTESIAN_POINT('Ctrl Pts',(16.6170000979997,-18.9526441512856,
9.29097292592683));
#175464=CARTESIAN_POINT('Ctrl Pts',(16.6170000985829,-18.9526460648981,
9.29097281413902));
#175465=CARTESIAN_POINT('Ctrl Pts',(16.6169387608845,-18.7516571212849,
9.30271402210781));
#175466=CARTESIAN_POINT('Ctrl Pts',(16.6454993572956,-18.5516397308117,
9.31315827170977));
#175467=CARTESIAN_POINT('Ctrl Pts',(16.7149206738938,-18.3138947250748,
9.32683236820389));
#175468=CARTESIAN_POINT('Ctrl Pts',(16.7294486235981,-18.2696284571598,
9.32943042288601));
#175469=CARTESIAN_POINT('Ctrl Pts',(16.7454193880554,-18.2258897123729,
9.33206801777758));
#175470=CARTESIAN_POINT('Origin',(18.734,-18.952,0.));
#175471=CARTESIAN_POINT('',(16.7454193692319,-18.2258897639242,10.3555828645479));
#175472=CARTESIAN_POINT('',(16.7454193829761,-18.2258897262833,10.1325348909312));
#175473=CARTESIAN_POINT('',(16.7454193692319,-18.2258897639242,0.));
#175474=CARTESIAN_POINT('',(16.6146463628246,-18.9530771010625,10.3109437268626));
#175475=CARTESIAN_POINT('Ctrl Pts',(16.6170002731508,-18.9530754163976,
10.3109437563772));
#175476=CARTESIAN_POINT('Ctrl Pts',(16.6169638477093,-18.8813704936142,
10.3152783077143));
#175477=CARTESIAN_POINT('Ctrl Pts',(16.6205747319161,-18.8095176190282,
10.3196128590514));
#175478=CARTESIAN_POINT('Ctrl Pts',(16.6278517403648,-18.7379240591854,
10.3239474103886));
#175479=CARTESIAN_POINT('Ctrl Pts',(16.6351199717668,-18.6664168507633,
10.3282767336763));
#175480=CARTESIAN_POINT('Ctrl Pts',(16.6460455147318,-18.5951688250439,
10.3326060569641));
#175481=CARTESIAN_POINT('Ctrl Pts',(16.6605951836021,-18.5245874740512,
10.3369353802518));
#175482=CARTESIAN_POINT('Ctrl Pts',(16.675130891217,-18.454073849979,10.3412605493015));
#175483=CARTESIAN_POINT('Ctrl Pts',(16.6932837245189,-18.384226113485,10.3455857183512));
#175484=CARTESIAN_POINT('Ctrl Pts',(16.7149688972722,-18.3154448914527,
10.3499108874009));
#175485=CARTESIAN_POINT('Ctrl Pts',(16.7244481263206,-18.2853785892241,
10.3518015464499));
#175486=CARTESIAN_POINT('Ctrl Pts',(16.7346016608924,-18.2555159614414,
10.3536922054989));
#175487=CARTESIAN_POINT('Ctrl Pts',(16.7454193692319,-18.2258897639242,
10.3555828645479));
#175488=CARTESIAN_POINT('Ctrl Pts',(16.7437494325541,-18.2252642451362,
9.55561791118868));
#175489=CARTESIAN_POINT('Ctrl Pts',(16.9543732025563,-17.6645819652671,
9.5917275247594));
#175490=CARTESIAN_POINT('Ctrl Pts',(17.9482900541193,-16.6327269270279,
9.67022907389064));
#175491=CARTESIAN_POINT('Ctrl Pts',(20.2082247500812,-16.9288855714836,
9.79112255858232));
#175492=CARTESIAN_POINT('Ctrl Pts',(21.2330889659179,-19.0965162449377,
9.91829836526374));
#175493=CARTESIAN_POINT('Ctrl Pts',(19.9651941664792,-21.1315622333512,
10.0454741719452));
#175494=CARTESIAN_POINT('Ctrl Pts',(17.5677551358241,-21.1669951515536,
10.1726499786266));
#175495=CARTESIAN_POINT('Ctrl Pts',(16.6440836935421,-19.7776853836357,
10.2611398283041));
#175496=CARTESIAN_POINT('Ctrl Pts',(16.6137958948767,-19.014466075178,10.307237742421));
#175497=CARTESIAN_POINT('Ctrl Pts',(16.614176999282,-18.9530774369802,10.3109437209775));
#175498=CARTESIAN_POINT('Ctrl Pts',(16.7454193880554,-18.2258897123729,
9.33206801777758));
#175499=CARTESIAN_POINT('Ctrl Pts',(16.7596276849878,-18.1869777945967,
9.33441453860362));
#175500=CARTESIAN_POINT('Ctrl Pts',(16.7749779213659,-18.1484833900871,
9.33679229479106));
#175501=CARTESIAN_POINT('Ctrl Pts',(16.799599094585,-18.0916499580595,9.34040226076874));
#175502=CARTESIAN_POINT('Ctrl Pts',(16.8080187823558,-18.0729633890997,
9.34160562443898));
#175503=CARTESIAN_POINT('Ctrl Pts',(16.8204632264257,-18.0463817313513,
9.34334229753595));
#175504=CARTESIAN_POINT('Ctrl Pts',(16.8242684619941,-18.0383847191264,
9.34386803505926));
#175505=CARTESIAN_POINT('Ctrl Pts',(16.8309529325593,-18.0245610010983,
9.34478260677337));
#175506=CARTESIAN_POINT('Ctrl Pts',(16.8338090477498,-18.0187232023072,
9.34517063272239));
#175507=CARTESIAN_POINT('Ctrl Pts',(16.8393529215622,-18.0075226680877,
9.34591861534346));
#175508=CARTESIAN_POINT('Ctrl Pts',(16.842036684437,-18.0021580164354,9.3462784293009));
#175509=CARTESIAN_POINT('Ctrl Pts',(16.8491284318565,-17.9881314244748,
9.34722333745082));
#175510=CARTESIAN_POINT('Ctrl Pts',(16.8535732922065,-17.9794883800337,
9.34780972450416));
#175511=CARTESIAN_POINT('Ctrl Pts',(16.8692136776856,-17.9495837374694,
9.34985322993656));
#175512=CARTESIAN_POINT('Ctrl Pts',(16.8807112371142,-17.9284829859791,
9.35132099652751));
#175513=CARTESIAN_POINT('Ctrl Pts',(16.9645626868343,-17.7806426021488,
9.36179322854543));
#175514=CARTESIAN_POINT('Ctrl Pts',(17.0494805740375,-17.6615090250345,
9.37126514852381));
#175515=CARTESIAN_POINT('Ctrl Pts',(17.2364663648891,-17.4493967086943,
9.38992675272336));
#175516=CARTESIAN_POINT('Ctrl Pts',(17.3367292888721,-17.3557344181346,
9.39904432072308));
#175517=CARTESIAN_POINT('Ctrl Pts',(17.4554185362512,-17.2646708028595,
9.40841263101319));
#175518=CARTESIAN_POINT('Ctrl Pts',(17.465566973191,-17.2570285983539,9.40920310389339));
#175519=CARTESIAN_POINT('Ctrl Pts',(17.4812017559145,-17.2454740126953,
9.4104040915905));
#175520=CARTESIAN_POINT('Ctrl Pts',(17.4866388264741,-17.2414958371181,
9.41081866996757));
#175521=CARTESIAN_POINT('Ctrl Pts',(17.495628865917,-17.2349836993859,9.41149899437401));
#175522=CARTESIAN_POINT('Ctrl Pts',(17.4991707986244,-17.2324346809424,
9.4117657198194));
#175523=CARTESIAN_POINT('Ctrl Pts',(17.5060325439406,-17.2275286308589,
9.41227987360158));
#175524=CARTESIAN_POINT('Ctrl Pts',(17.5093513209997,-17.2251701908422,
9.41252739622004));
#175525=CARTESIAN_POINT('Ctrl Pts',(17.5126866069157,-17.2228144703318,
9.41277497694871));
#175526=CARTESIAN_POINT('Ctrl Pts',(17.5126963004708,-17.2228076238726,
9.41277569649852));
#175527=CARTESIAN_POINT('Ctrl Pts',(17.5127157223261,-17.2227939066588,
9.41277713815739));
#175528=CARTESIAN_POINT('Ctrl Pts',(17.5127254500437,-17.2227870363166,
9.41277786022313));
#175529=CARTESIAN_POINT('Ctrl Pts',(17.512744940083,-17.2227732714389,9.41277930690319));
#175530=CARTESIAN_POINT('Ctrl Pts',(17.5127547027751,-17.2227663766429,
9.41278003154492));
#175531=CARTESIAN_POINT('Ctrl Pts',(17.5127748948248,-17.2227521164816,
9.41278153029124));
#175532=CARTESIAN_POINT('Ctrl Pts',(17.5127853244933,-17.2227447509144,
9.41278230441747));
#175533=CARTESIAN_POINT('Ctrl Pts',(17.512806352193,-17.2227299011652,9.41278386514324));
#175534=CARTESIAN_POINT('Ctrl Pts',(17.5128169496939,-17.2227224173622,
9.41278465170306));
#175535=CARTESIAN_POINT('Ctrl Pts',(17.5128383163199,-17.2227073288522,
9.41278623753695));
#175536=CARTESIAN_POINT('Ctrl Pts',(17.5128490858015,-17.2226997238982,
9.41278703683709));
#175537=CARTESIAN_POINT('Ctrl Pts',(17.512870800011,-17.2226843905424,9.4127886484193));
#175538=CARTESIAN_POINT('Ctrl Pts',(17.5128817447291,-17.2226766621526,
9.41278946070024));
#175539=CARTESIAN_POINT('Ctrl Pts',(17.5129038132836,-17.2226610792063,
9.4127910985302));
#175540=CARTESIAN_POINT('Ctrl Pts',(17.5129149371519,-17.2226532246323,
9.41279192408116));
#175541=CARTESIAN_POINT('Ctrl Pts',(17.5129373680329,-17.2226373864903,
9.4127935887487));
#175542=CARTESIAN_POINT('Ctrl Pts',(17.5129486748447,-17.2226294030694,
9.41279442784993));
#175543=CARTESIAN_POINT('Ctrl Pts',(17.5129714756278,-17.2226133044147,
9.41279611991465));
#175544=CARTESIAN_POINT('Ctrl Pts',(17.5129829694858,-17.2226051892664,
9.4127969728693));
#175545=CARTESIAN_POINT('Ctrl Pts',(17.5130061483692,-17.2225888243439,
9.41279869293691));
#175546=CARTESIAN_POINT('Ctrl Pts',(17.5130178333919,-17.2225805745772,
9.41279956004922));
#175547=CARTESIAN_POINT('Ctrl Pts',(17.5130413986242,-17.2225639375976,
9.41280130872903));
#175548=CARTESIAN_POINT('Ctrl Pts',(17.5130532790921,-17.2225555502082,
9.41280219031522));
#175549=CARTESIAN_POINT('Ctrl Pts',(17.5130772396492,-17.2225386348704,
9.41280396827037));
#175550=CARTESIAN_POINT('Ctrl Pts',(17.5130893197452,-17.2225301069234,
9.41280486463933));
#175551=CARTESIAN_POINT('Ctrl Pts',(17.5131136840949,-17.2225129072868,
9.41280667249513));
#175552=CARTESIAN_POINT('Ctrl Pts',(17.5131259683995,-17.2225042355676,
9.41280758398522));
#175553=CARTESIAN_POINT('Ctrl Pts',(17.5131507459074,-17.2224867450594,
9.41280942243346));
#175554=CARTESIAN_POINT('Ctrl Pts',(17.5131632389502,-17.2224779263902,
9.41281034937916));
#175555=CARTESIAN_POINT('Ctrl Pts',(17.5131884386196,-17.2224601386953,
9.41281221908457));
#175556=CARTESIAN_POINT('Ctrl Pts',(17.513201145293,-17.2224511696434,9.41281316184721));
#175557=CARTESIAN_POINT('Ctrl Pts',(17.5132267769499,-17.2224330778677,
9.41281506353545));
#175558=CARTESIAN_POINT('Ctrl Pts',(17.5132397021304,-17.2224239550122,
9.41281602247508));
#175559=CARTESIAN_POINT('Ctrl Pts',(17.5132657758111,-17.2224055521155,
9.41281795688722));
#175560=CARTESIAN_POINT('Ctrl Pts',(17.5132789244848,-17.2223962719594,
9.41281893237198));
#175561=CARTESIAN_POINT('Ctrl Pts',(17.5161294850279,-17.2203844335687,
9.41303040817569));
#175562=CARTESIAN_POINT('Ctrl Pts',(17.5189717797181,-17.2183888886933,
9.41324041720716));
#175563=CARTESIAN_POINT('Ctrl Pts',(17.525590943879,-17.2137659189939,9.41372752539437));
#175564=CARTESIAN_POINT('Ctrl Pts',(17.5293714723193,-17.2111438087823,
9.41400426053556));
#175565=CARTESIAN_POINT('Ctrl Pts',(17.5410657491037,-17.2030891929109,
9.41485583718684));
#175566=CARTESIAN_POINT('Ctrl Pts',(17.5490080471362,-17.1976980825398,
9.41542793908332));
#175567=CARTESIAN_POINT('Ctrl Pts',(17.6515166969557,-17.1291305937148,
9.42273564472652));
#175568=CARTESIAN_POINT('Ctrl Pts',(17.7510022998792,-17.0736108423631,
9.4290038457494));
#175569=CARTESIAN_POINT('Ctrl Pts',(17.9581854581276,-16.9789821990892,
9.44141734454648));
#175570=CARTESIAN_POINT('Ctrl Pts',(18.0655443869056,-16.9400721317457,
9.4475464669605));
#175571=CARTESIAN_POINT('Ctrl Pts',(18.2286276583947,-16.8954689386177,
9.45694786152188));
#175572=CARTESIAN_POINT('Ctrl Pts',(18.2822857600101,-16.8830208286609,
9.4600529683545));
#175573=CARTESIAN_POINT('Ctrl Pts',(18.3700426733623,-16.8662388210013,
9.46519334628232));
#175574=CARTESIAN_POINT('Ctrl Pts',(18.4038698619593,-16.860618034139,9.46718930263892));
#175575=CARTESIAN_POINT('Ctrl Pts',(18.4485175927613,-16.8543094656963,
9.46984862841864));
#175576=CARTESIAN_POINT('Ctrl Pts',(18.4592291698385,-16.8528795253993,
9.4704884993312));
#175577=CARTESIAN_POINT('Ctrl Pts',(18.4767948791167,-16.8506713480323,
9.47154104010516));
#175578=CARTESIAN_POINT('Ctrl Pts',(18.4836427812187,-16.8498444779081,
9.47195216963619));
#175579=CARTESIAN_POINT('Ctrl Pts',(18.4969087207802,-16.8483083831865,
9.47275022105392));
#175580=CARTESIAN_POINT('Ctrl Pts',(18.5033262097073,-16.8475950260531,
9.47313700777826));
#175581=CARTESIAN_POINT('Ctrl Pts',(18.5181552073712,-16.8460153065518,
9.4740324762627));
#175582=CARTESIAN_POINT('Ctrl Pts',(18.5265688017917,-16.845169964541,9.47454181456681));
#175583=CARTESIAN_POINT('Ctrl Pts',(18.5492181256979,-16.8430312981077,
9.47591646886654));
#175584=CARTESIAN_POINT('Ctrl Pts',(18.5634620726007,-16.8418317303546,
9.47678471522296));
#175585=CARTESIAN_POINT('Ctrl Pts',(18.6945796772711,-16.8321257573915,
9.4848126999604));
#175586=CARTESIAN_POINT('Ctrl Pts',(18.8119397005935,-16.8331941337924,
9.49227603027375));
#175587=CARTESIAN_POINT('Ctrl Pts',(19.0917049283942,-16.8590192387907,
9.51063007243621));
#175588=CARTESIAN_POINT('Ctrl Pts',(19.2525142793748,-16.8929554484554,
9.52166370538066));
#175589=CARTESIAN_POINT('Ctrl Pts',(19.437425977985,-16.955037959666,9.53404313472439));
#175590=CARTESIAN_POINT('Ctrl Pts',(19.4668278890122,-16.965639251686,9.53599994777887));
#175591=CARTESIAN_POINT('Ctrl Pts',(19.5026583171494,-16.979462411726,9.53836109540091));
#175592=CARTESIAN_POINT('Ctrl Pts',(19.509317636307,-16.9820703789543,9.5387989181054));
#175593=CARTESIAN_POINT('Ctrl Pts',(19.5197647541113,-16.9862229318375,
9.53948403360274));
#175594=CARTESIAN_POINT('Ctrl Pts',(19.5235614386363,-16.9877448063477,
9.53973265515284));
#175595=CARTESIAN_POINT('Ctrl Pts',(19.5306680435971,-16.990617373441,9.54019730998764));
#175596=CARTESIAN_POINT('Ctrl Pts',(19.5339789155852,-16.9919654303331,
9.54041349149122));
#175597=CARTESIAN_POINT('Ctrl Pts',(19.5415527401777,-16.9950715816339,
9.54090736211619));
#175598=CARTESIAN_POINT('Ctrl Pts',(19.5458133664464,-16.9968352187708,
9.54118471203861));
#175599=CARTESIAN_POINT('Ctrl Pts',(19.5589743308678,-17.0023334860903,
9.54204006799652));
#175600=CARTESIAN_POINT('Ctrl Pts',(19.5678550600484,-17.0061151347389,
9.54261529912772));
#175601=CARTESIAN_POINT('Ctrl Pts',(19.6762368192341,-17.0531451917887,
9.54961529955773));
#175602=CARTESIAN_POINT('Ctrl Pts',(19.772311207705,-17.1039263668871,9.55561523347598));
#175603=CARTESIAN_POINT('Ctrl Pts',(19.9635525619985,-17.2246529631629,
9.5679577273629));
#175604=CARTESIAN_POINT('Ctrl Pts',(20.0576162106425,-17.2956284133548,
9.57427145519332));
#175605=CARTESIAN_POINT('Ctrl Pts',(20.2026253366148,-17.4253225178517,
9.58508081897925));
#175606=CARTESIAN_POINT('Ctrl Pts',(20.2571115128213,-17.4796773391617,
9.5894377876174));
#175607=CARTESIAN_POINT('Ctrl Pts',(20.3212568871287,-17.5510475246551,
9.59503928573504));
#175608=CARTESIAN_POINT('Ctrl Pts',(20.3338050359408,-17.5653940445243,
9.59615951109523));
#175609=CARTESIAN_POINT('Ctrl Pts',(20.3517317035072,-17.5864572127967,
9.59779691111755));
#175610=CARTESIAN_POINT('Ctrl Pts',(20.3572659078999,-17.5930405608937,
9.59830767244357));
#175611=CARTESIAN_POINT('Ctrl Pts',(20.3668841974132,-17.6046248168695,
9.59920475171686));
#175612=CARTESIAN_POINT('Ctrl Pts',(20.3709858310344,-17.6096110571651,
9.59959034826484));
#175613=CARTESIAN_POINT('Ctrl Pts',(20.3788956225875,-17.6193169292136,
9.60033992786648));
#175614=CARTESIAN_POINT('Ctrl Pts',(20.3827064404254,-17.6240343195407,
9.60070379805627));
#175615=CARTESIAN_POINT('Ctrl Pts',(20.3917517061395,-17.6353303533347,
9.60157406586847));
#175616=CARTESIAN_POINT('Ctrl Pts',(20.3969673088234,-17.6419238937171,
9.60208121175134));
#175617=CARTESIAN_POINT('Ctrl Pts',(20.4155535289775,-17.6657103371306,
9.60390790801144));
#175618=CARTESIAN_POINT('Ctrl Pts',(20.4286975572695,-17.683077819019,9.60523636842149));
#175619=CARTESIAN_POINT('Ctrl Pts',(20.5531443718273,-17.8528950794568,
9.61817956209638));
#175620=CARTESIAN_POINT('Ctrl Pts',(20.6438341549979,-18.0193573318385,
9.63062523874681));
#175621=CARTESIAN_POINT('Ctrl Pts',(20.7391536177478,-18.2685188771991,
9.64823217801498));
#175622=CARTESIAN_POINT('Ctrl Pts',(20.7630014530789,-18.3429497318971,
9.65335810412934));
#175623=CARTESIAN_POINT('Ctrl Pts',(20.7916212284576,-18.4528586818725,
9.66059443667281));
#175624=CARTESIAN_POINT('Ctrl Pts',(20.7996960862217,-18.4874064167957,
9.6628221232846));
#175625=CARTESIAN_POINT('Ctrl Pts',(20.8084084945525,-18.5294202636081,
9.66546171145211));
#175626=CARTESIAN_POINT('Ctrl Pts',(20.8098792731637,-18.536705546754,9.66591690937895));
#175627=CARTESIAN_POINT('Ctrl Pts',(20.8121118488182,-18.5480725540374,
9.6666230683348));
#175628=CARTESIAN_POINT('Ctrl Pts',(20.812900039275,-18.5521489462482,9.66687549378249));
#175629=CARTESIAN_POINT('Ctrl Pts',(20.8143430189101,-18.5597314128401,
9.66734348113989));
#175630=CARTESIAN_POINT('Ctrl Pts',(20.815000933894,-18.5632367890323,9.66755921409265));
#175631=CARTESIAN_POINT('Ctrl Pts',(20.8164726651625,-18.5711889780945,
9.66804723326561));
#175632=CARTESIAN_POINT('Ctrl Pts',(20.8172810968247,-18.5756367339425,
9.66831921076136));
#175633=CARTESIAN_POINT('Ctrl Pts',(20.8196378665154,-18.5888432813987,
9.66912397475711));
#175634=CARTESIAN_POINT('Ctrl Pts',(20.8211452811711,-18.5976094046622,
9.66965449267586));
#175635=CARTESIAN_POINT('Ctrl Pts',(20.8320582462934,-18.6635578936841,
9.67361991007654));
#175636=CARTESIAN_POINT('Ctrl Pts',(20.8391684225418,-18.7211007988519,
9.67693496138901));
#175637=CARTESIAN_POINT('Ctrl Pts',(20.857158271779,-18.9403378880945,9.68926003309523));
#175638=CARTESIAN_POINT('Ctrl Pts',(20.8518296659783,-19.1028006017573,
9.69780683165734));
#175639=CARTESIAN_POINT('Ctrl Pts',(20.8190932103625,-19.3231690468967,
9.71014097930096));
#175640=CARTESIAN_POINT('Ctrl Pts',(20.8075836130097,-19.3828483879239,
9.71355275612229));
#175641=CARTESIAN_POINT('Ctrl Pts',(20.7850065449133,-19.4777525340239,
9.71915322129601));
#175642=CARTESIAN_POINT('Ctrl Pts',(20.7755568386602,-19.5133278968979,
9.72129270112995));
#175643=CARTESIAN_POINT('Ctrl Pts',(20.7620605955166,-19.5592743434434,
9.72411575837883));
#175644=CARTESIAN_POINT('Ctrl Pts',(20.75885264916,-19.5698864373096,9.72477198317596));
#175645=CARTESIAN_POINT('Ctrl Pts',(20.7534955477933,-19.5871182282838,
9.72584458650863));
#175646=CARTESIAN_POINT('Ctrl Pts',(20.7513968153266,-19.5937534722835,
9.72625930788545));
#175647=CARTESIAN_POINT('Ctrl Pts',(20.747294749064,-19.6065033649665,9.72705955127081));
#175648=CARTESIAN_POINT('Ctrl Pts',(20.745296176942,-19.6126194733447,9.7274449126698));
#175649=CARTESIAN_POINT('Ctrl Pts',(20.7406517755257,-19.62661600391,9.72833025288092));
#175650=CARTESIAN_POINT('Ctrl Pts',(20.7379873633738,-19.6344901063839,
9.72883084148726));
#175651=CARTESIAN_POINT('Ctrl Pts',(20.7307755624286,-19.6553966698757,
9.73016676218824));
#175652=CARTESIAN_POINT('Ctrl Pts',(20.7261470296075,-19.6684005305464,
9.73100477326359));
#175653=CARTESIAN_POINT('Ctrl Pts',(20.6892292403148,-19.7689960043559,
9.73754353809784));
#175654=CARTESIAN_POINT('Ctrl Pts',(20.6513096232959,-19.8543987811313,
9.7434332824999));
#175655=CARTESIAN_POINT('Ctrl Pts',(20.5249511349982,-20.0947827722979,
9.76099378517052));
#175656=CARTESIAN_POINT('Ctrl Pts',(20.4224349717483,-20.241433728627,9.77303670911449));
#175657=CARTESIAN_POINT('Ctrl Pts',(20.2755389873639,-20.4035476333015,
9.78703587150884));
#175658=CARTESIAN_POINT('Ctrl Pts',(20.2474538429422,-20.4328075309318,
9.78959089361936));
#175659=CARTESIAN_POINT('Ctrl Pts',(20.213039365163,-20.4666587616583,9.79256230445));
#175660=CARTESIAN_POINT('Ctrl Pts',(20.2075055322638,-20.4720427818222,
9.79303538636506));
#175661=CARTESIAN_POINT('Ctrl Pts',(20.1989055518307,-20.480318843031,9.79376315314813));
#175662=CARTESIAN_POINT('Ctrl Pts',(20.1958600814827,-20.4832321393666,
9.79401944785775));
#175663=CARTESIAN_POINT('Ctrl Pts',(20.1902250503846,-20.4885904744419,
9.79449101119004));
#175664=CARTESIAN_POINT('Ctrl Pts',(20.187638039065,-20.4910380551589,9.79470647361805));
#175665=CARTESIAN_POINT('Ctrl Pts',(20.1818122150451,-20.4965220940686,
9.79518938685155));
#175666=CARTESIAN_POINT('Ctrl Pts',(20.1785700305081,-20.4995548897806,
9.7954565563493));
#175667=CARTESIAN_POINT('Ctrl Pts',(20.1702614301382,-20.5072780366454,
9.79613726570796));
#175668=CARTESIAN_POINT('Ctrl Pts',(20.1651815215219,-20.5119538847005,
9.79654972254341));
#175669=CARTESIAN_POINT('Ctrl Pts',(20.1355914857509,-20.5389240942688,
9.79893134219442));
#175670=CARTESIAN_POINT('Ctrl Pts',(20.1105820799534,-20.560666784958,9.80086164003915));
#175671=CARTESIAN_POINT('Ctrl Pts',(20.0710469395953,-20.5934403161374,
9.80380627737103));
#175672=CARTESIAN_POINT('Ctrl Pts',(20.0568729890853,-20.604884726693,9.80484155601451));
#175673=CARTESIAN_POINT('Ctrl Pts',(20.0413800411324,-20.6170671618631,
9.80595343800128));
#175674=CARTESIAN_POINT('Ctrl Pts',(20.040206381039,-20.6179880298538,9.80603754692448));
#175675=CARTESIAN_POINT('Ctrl Pts',(20.0209856109252,-20.6330360830935,
9.80741301737463));
#175676=CARTESIAN_POINT('Ctrl Pts',(20.0027107691817,-20.6468708836604,
9.8086925189548));
#175677=CARTESIAN_POINT('Ctrl Pts',(19.9473564856489,-20.6873792305149,
9.81249592546884));
#175678=CARTESIAN_POINT('Ctrl Pts',(19.9096342252567,-20.7131528723076,
9.8149933681089));
#175679=CARTESIAN_POINT('Ctrl Pts',(19.7788703607878,-20.7964219471259,
9.82343360672363));
#175680=CARTESIAN_POINT('Ctrl Pts',(19.6822226017222,-20.8479217820874,
9.82932170052626));
#175681=CARTESIAN_POINT('Ctrl Pts',(19.5315380753926,-20.913799976287,9.83846604524153));
#175682=CARTESIAN_POINT('Ctrl Pts',(19.4802031270367,-20.9338946431348,
9.84157356654434));
#175683=CARTESIAN_POINT('Ctrl Pts',(19.3957342438674,-20.9632120244641,
9.84671758500308));
#175684=CARTESIAN_POINT('Ctrl Pts',(19.363056050306,-20.973671166593,9.84871469434997));
#175685=CARTESIAN_POINT('Ctrl Pts',(19.319767937305,-20.9863750284397,9.85137533855444));
#175686=CARTESIAN_POINT('Ctrl Pts',(19.3093734142952,-20.9893392599853,
9.85201534514958));
#175687=CARTESIAN_POINT('Ctrl Pts',(19.2923087886658,-20.9940646124243,
9.85306805225241));
#175688=CARTESIAN_POINT('Ctrl Pts',(19.2856518901842,-20.9958729841019,
9.85347921147363));
#175689=CARTESIAN_POINT('Ctrl Pts',(19.2727471210776,-20.9993109754522,
9.85427727988268));
#175690=CARTESIAN_POINT('Ctrl Pts',(19.2665003924563,-21.0009446115689,
9.85466405369288));
#175691=CARTESIAN_POINT('Ctrl Pts',(19.2520570035944,-21.004651315581,9.85555943306801));
#175692=CARTESIAN_POINT('Ctrl Pts',(19.2438552437113,-21.0067038982662,
9.85606869476603));
#175693=CARTESIAN_POINT('Ctrl Pts',(19.2217585237242,-21.0120934021167,
9.85744300828095));
#175694=CARTESIAN_POINT('Ctrl Pts',(19.2078418939486,-21.0153388104556,
9.85831098819905));
#175695=CARTESIAN_POINT('Ctrl Pts',(19.0798345003788,-21.0438272797968,
9.86631834025349));
#175696=CARTESIAN_POINT('Ctrl Pts',(18.9638883005151,-21.0597206722713,
9.87375949716051));
#175697=CARTESIAN_POINT('Ctrl Pts',(18.6847491590449,-21.0746733430815,
9.89201886092508));
#175698=CARTESIAN_POINT('Ctrl Pts',(18.5218018231455,-21.0646144403409,
9.90297712326021));
#175699=CARTESIAN_POINT('Ctrl Pts',(18.3296136859093,-21.0302727317604,
9.91538262508376));
#175700=CARTESIAN_POINT('Ctrl Pts',(18.2977453968435,-21.0238175663966,
9.91742015007815));
#175701=CARTESIAN_POINT('Ctrl Pts',(18.2589759004651,-21.0150301786804,
9.91986466572181));
#175702=CARTESIAN_POINT('Ctrl Pts',(18.2519234288635,-21.013393605388,9.92030794431918));
#175703=CARTESIAN_POINT('Ctrl Pts',(18.2408808805105,-21.0107713383333,
9.92099967250386));
#175704=CARTESIAN_POINT('Ctrl Pts',(18.236885119741,-21.0098101676388,9.92124949285123));
#175705=CARTESIAN_POINT('Ctrl Pts',(18.2294217708606,-21.0079918698817,
9.92171517610271));
#175706=CARTESIAN_POINT('Ctrl Pts',(18.2259535912148,-21.0071376122031,
9.92193119447293));
#175707=CARTESIAN_POINT('Ctrl Pts',(18.2180419437898,-21.0051676192209,
9.92242312163059));
#175708=CARTESIAN_POINT('Ctrl Pts',(18.2135999339337,-21.0040462374247,
9.9226987012499));
#175709=CARTESIAN_POINT('Ctrl Pts',(18.1999587797943,-21.00055539645,9.92354320032073));
#175710=CARTESIAN_POINT('Ctrl Pts',(18.1907717693831,-20.9981383956788,
9.92410944563108));
#175711=CARTESIAN_POINT('Ctrl Pts',(18.108445438004,-20.9758856822973,9.92916368761632));
#175712=CARTESIAN_POINT('Ctrl Pts',(18.0363956240174,-20.9521956140284,
9.93344589650438));
#175713=CARTESIAN_POINT('Ctrl Pts',(17.9259442317426,-20.9091819038263,
9.94000667512318));
#175714=CARTESIAN_POINT('Ctrl Pts',(17.8866016392593,-20.8924719358181,
9.94234269522203));
#175715=CARTESIAN_POINT('Ctrl Pts',(17.748509231106,-20.828818611868,9.95062116095358));
#175716=CARTESIAN_POINT('Ctrl Pts',(17.6529225571144,-20.7754338027292,
9.95650785989923));
#175717=CARTESIAN_POINT('Ctrl Pts',(17.5160260225288,-20.6844149999887,
9.96564896184914));
#175718=CARTESIAN_POINT('Ctrl Pts',(17.4713725018903,-20.6521451404657,
9.96875462450005));
#175719=CARTESIAN_POINT('Ctrl Pts',(17.4010406010917,-20.5970179911439,
9.97389584051523));
#175720=CARTESIAN_POINT('Ctrl Pts',(17.37457038908,-20.5752115964785,9.97589206232658));
#175721=CARTESIAN_POINT('Ctrl Pts',(17.3404706757043,-20.5457006671356,
9.97855169165393));
#175722=CARTESIAN_POINT('Ctrl Pts',(17.3323532377909,-20.5385661478596,
9.97919159381127));
#175723=CARTESIAN_POINT('Ctrl Pts',(17.3191448626728,-20.5267766571123,
9.98024417288709));
#175724=CARTESIAN_POINT('Ctrl Pts',(17.314021357719,-20.5221583465184,9.98065530925501));
#175725=CARTESIAN_POINT('Ctrl Pts',(17.3041456362353,-20.5131685338695,
9.98145336458347));
#175726=CARTESIAN_POINT('Ctrl Pts',(17.2993906642057,-20.5088001621725,
9.98184014833224));
#175727=CARTESIAN_POINT('Ctrl Pts',(17.2884551799496,-20.4986611367334,
9.98273559628881));
#175728=CARTESIAN_POINT('Ctrl Pts',(17.2822891391559,-20.4928750993909,
9.98324491694591));
#175729=CARTESIAN_POINT('Ctrl Pts',(17.2657938265297,-20.4772094709614,
9.98461949273961));
#175730=CARTESIAN_POINT('Ctrl Pts',(17.2555298121516,-20.4672620849351,
9.98548767771643));
#175731=CARTESIAN_POINT('Ctrl Pts',(17.1621045911684,-20.3748659001916,
9.99351084267146));
#175732=CARTESIAN_POINT('Ctrl Pts',(17.0858313941751,-20.2857671975202,
10.0009689917939));
#175733=CARTESIAN_POINT('Ctrl Pts',(16.9216222301059,-20.0582193023279,
10.0193000830356));
#175734=CARTESIAN_POINT('Ctrl Pts',(16.8416122337423,-19.9149657665934,
10.0303152198449));
#175735=CARTESIAN_POINT('Ctrl Pts',(16.7667878036911,-19.7347904076777,
10.0427007538937));
#175736=CARTESIAN_POINT('Ctrl Pts',(16.7553382284179,-19.7053807060988,
10.0446770876979));
#175737=CARTESIAN_POINT('Ctrl Pts',(16.742097493446,-19.6689831662001,10.047058431303));
#175738=CARTESIAN_POINT('Ctrl Pts',(16.7396794444265,-19.6622295271547,
10.0474975967757));
#175739=CARTESIAN_POINT('Ctrl Pts',(16.7359349675651,-19.6516012405593,
10.0481843401434));
#175740=CARTESIAN_POINT('Ctrl Pts',(16.7345854008489,-19.6477348855633,
10.0484332570824));
#175741=CARTESIAN_POINT('Ctrl Pts',(16.7320789915784,-19.6404867827741,
10.0488981633403));
#175742=CARTESIAN_POINT('Ctrl Pts',(16.7309195071483,-19.6371060599562,
10.0491143026685));
#175743=CARTESIAN_POINT('Ctrl Pts',(16.7282860719902,-19.6293638851444,
10.0496076853711));
#175744=CARTESIAN_POINT('Ctrl Pts',(16.7268177853927,-19.6250005588354,
10.0498845920573));
#175745=CARTESIAN_POINT('Ctrl Pts',(16.7223273455718,-19.6115108447702,
10.050737222297));
#175746=CARTESIAN_POINT('Ctrl Pts',(16.7193530677632,-19.6023684872821,
10.0513101964217));
#175747=CARTESIAN_POINT('Ctrl Pts',(16.6905474223959,-19.5117313338043,
10.0569454309902));
#175748=CARTESIAN_POINT('Ctrl Pts',(16.6696095020876,-19.4287525817019,
10.0617451503291));
#175749=CARTESIAN_POINT('Ctrl Pts',(16.6294008321654,-19.2157687439358,
10.0736795303986));
#175750=CARTESIAN_POINT('Ctrl Pts',(16.6170990832059,-19.0848277878281,
10.0806785850671));
#175751=CARTESIAN_POINT('Ctrl Pts',(16.6169313786705,-18.8613529308207,
10.0930378829247));
#175752=CARTESIAN_POINT('Ctrl Pts',(16.6228899854673,-18.7692216646518,
10.0982490862488));
#175753=CARTESIAN_POINT('Ctrl Pts',(16.6366195100423,-18.6641219266842,
10.104462743823));
#175754=CARTESIAN_POINT('Ctrl Pts',(16.6385368154061,-18.6504826151109,
10.1052742404711));
#175755=CARTESIAN_POINT('Ctrl Pts',(16.641823177128,-18.6286517383975,10.106581719328));
#175756=CARTESIAN_POINT('Ctrl Pts',(16.6431076017403,-18.6204476928975,
10.1070750246083));
#175757=CARTESIAN_POINT('Ctrl Pts',(16.6454726643887,-18.6059018161945,
10.107953215884));
#175758=CARTESIAN_POINT('Ctrl Pts',(16.6465340099925,-18.5995569215029,
10.1083374851181));
#175759=CARTESIAN_POINT('Ctrl Pts',(16.6488043601941,-18.5863545015927,
10.1091396183901));
#175760=CARTESIAN_POINT('Ctrl Pts',(16.6500183104995,-18.5794979157171,
10.1095576355982));
#175761=CARTESIAN_POINT('Ctrl Pts',(16.6532558814742,-18.5617228935686,
10.110645087726));
#175762=CARTESIAN_POINT('Ctrl Pts',(16.6553316014101,-18.5508142725261,
10.1113161754137));
#175763=CARTESIAN_POINT('Ctrl Pts',(16.6646897604107,-18.5036573919809,
10.1142336488192));
#175764=CARTESIAN_POINT('Ctrl Pts',(16.6728349138898,-18.467588832413,10.116507408672));
#175765=CARTESIAN_POINT('Ctrl Pts',(16.6969459033728,-18.3724844854234,
10.1226194523867));
#175766=CARTESIAN_POINT('Ctrl Pts',(16.7145313844524,-18.3138988809202,
10.1265064270926));
#175767=CARTESIAN_POINT('Ctrl Pts',(16.7381478933373,-18.2460409537553,
10.1311462799043));
#175768=CARTESIAN_POINT('Ctrl Pts',(16.7417458099075,-18.2359504518563,
10.1318398405155));
#175769=CARTESIAN_POINT('Ctrl Pts',(16.7454193829761,-18.2258897262833,
10.1325348909312));
#175770=CARTESIAN_POINT('Origin',(18.734,-18.952,0.));
#175771=CARTESIAN_POINT('',(16.7454193125898,-18.2258899190485,11.1558808694255));
#175772=CARTESIAN_POINT('',(16.7454193692319,-18.2258897639242,10.9336112441224));
#175773=CARTESIAN_POINT('',(16.7454193692319,-18.2258897639242,0.));
#175774=CARTESIAN_POINT('',(16.6170004031077,-18.9533064294667,11.1109437209282));
#175775=CARTESIAN_POINT('Ctrl Pts',(16.7454193125899,-18.2258899190484,
11.1558808694255));
#175776=CARTESIAN_POINT('Ctrl Pts',(16.7234360607655,-18.2860949364022,
11.1523878540446));
#175777=CARTESIAN_POINT('Ctrl Pts',(16.7041774484112,-18.3473239923796,
11.1488669690875));
#175778=CARTESIAN_POINT('Ctrl Pts',(16.6773854477283,-18.4483623928592,
11.1430184399809));
#175779=CARTESIAN_POINT('Ctrl Pts',(16.6681681730665,-18.4876156162813,
11.1407373991175));
#175780=CARTESIAN_POINT('Ctrl Pts',(16.6588573176701,-18.5330622867407,
11.1380746208254));
#175781=CARTESIAN_POINT('Ctrl Pts',(16.6576628095842,-18.5390232085414,
11.1377249391111));
#175782=CARTESIAN_POINT('Ctrl Pts',(16.6558534146321,-18.5482589055261,
11.1371824507173));
#175783=CARTESIAN_POINT('Ctrl Pts',(16.6552205494197,-18.5515301542999,
11.1369901675784));
#175784=CARTESIAN_POINT('Ctrl Pts',(16.6491723940305,-18.5831934296378,
11.1351276504799));
#175785=CARTESIAN_POINT('Ctrl Pts',(16.6443315832669,-18.611690990428,11.1334407270184));
#175786=CARTESIAN_POINT('Ctrl Pts',(16.638532301595,-18.6506463611421,11.1311167916703));
#175787=CARTESIAN_POINT('Ctrl Pts',(16.6370657847835,-18.6610261493246,
11.1304958503707));
#175788=CARTESIAN_POINT('Ctrl Pts',(16.634862067329,-18.6775064781172,11.1295070779318));
#175789=CARTESIAN_POINT('Ctrl Pts',(16.6340742205913,-18.6836001607958,
11.1291408506994));
#175790=CARTESIAN_POINT('Ctrl Pts',(16.6325483605536,-18.6958202122398,
11.1284051467365));
#175791=CARTESIAN_POINT('Ctrl Pts',(16.6318105825134,-18.7019465490214,
11.1280356664325));
#175792=CARTESIAN_POINT('Ctrl Pts',(16.6303836083735,-18.7142486765774,
11.1272923938588));
#175793=CARTESIAN_POINT('Ctrl Pts',(16.6296947991971,-18.7204244496969,
11.126918593272));
#175794=CARTESIAN_POINT('Ctrl Pts',(16.6281826815492,-18.7345460177625,
11.1260622899236));
#175795=CARTESIAN_POINT('Ctrl Pts',(16.6273771405484,-18.7424935839338,
11.1255792320414));
#175796=CARTESIAN_POINT('Ctrl Pts',(16.6254321889814,-18.7628293109863,
11.1243402456562));
#175797=CARTESIAN_POINT('Ctrl Pts',(16.6243569717784,-18.7752231736112,
11.1235823147682));
#175798=CARTESIAN_POINT('Ctrl Pts',(16.6190952486443,-18.8427850268363,
11.1194348782796));
#175799=CARTESIAN_POINT('Ctrl Pts',(16.6169637969027,-18.8980864419166,
11.1159819897524));
#175800=CARTESIAN_POINT('Ctrl Pts',(16.6170004651092,-18.9534033075656,
11.1124693548963));
#175801=CARTESIAN_POINT('Ctrl Pts',(16.7454193692319,-18.2258897639242,
10.3555828645479));
#175802=CARTESIAN_POINT('Ctrl Pts',(16.7701522594713,-18.1581543925862,
10.3599055418906));
#175803=CARTESIAN_POINT('Ctrl Pts',(16.7983602529091,-18.091656257472,10.3642282192334));
#175804=CARTESIAN_POINT('Ctrl Pts',(16.8298869258318,-18.0267744054655,
10.3685508965761));
#175805=CARTESIAN_POINT('Ctrl Pts',(16.8614136604731,-17.9618924264424,
10.3728735823811));
#175806=CARTESIAN_POINT('Ctrl Pts',(16.896258868959,-17.8986271805337,10.3771962681862));
#175807=CARTESIAN_POINT('Ctrl Pts',(16.9342193564648,-17.8373347430031,
10.3815189539912));
#175808=CARTESIAN_POINT('Ctrl Pts',(16.972217854968,-17.7759809314797,10.3858459682338));
#175809=CARTESIAN_POINT('Ctrl Pts',(17.0133375966607,-17.7166042917782,
10.3901729824764));
#175810=CARTESIAN_POINT('Ctrl Pts',(17.0573316320686,-17.6595325211139,
10.394499996719));
#175811=CARTESIAN_POINT('Ctrl Pts',(17.1013502294102,-17.6024288871973,
10.3988294267399));
#175812=CARTESIAN_POINT('Ctrl Pts',(17.1482459902095,-17.5476330570704,
10.4031588567608));
#175813=CARTESIAN_POINT('Ctrl Pts',(17.1977330353864,-17.4954380159303,
10.4074882867817));
#175814=CARTESIAN_POINT('Ctrl Pts',(17.2473041777985,-17.4431542756441,
10.4118250741442));
#175815=CARTESIAN_POINT('Ctrl Pts',(17.2994750328197,-17.3934804831633,
10.4161618615067));
#175816=CARTESIAN_POINT('Ctrl Pts',(17.3539250843281,-17.3466706795386,
10.4204986488692));
#175817=CARTESIAN_POINT('Ctrl Pts',(17.3811407440825,-17.3232738295205,
10.422666296576));
#175818=CARTESIAN_POINT('Ctrl Pts',(17.4089253292483,-17.3005918231404,
10.4248339442827));
#175819=CARTESIAN_POINT('Ctrl Pts',(17.4372361998844,-17.2786522636614,
10.4270015919895));
#175820=CARTESIAN_POINT('Ctrl Pts',(17.494549025663,-17.2342375875375,10.4313898009204));
#175821=CARTESIAN_POINT('Ctrl Pts',(17.5542581954978,-17.1926841015565,
10.4357780098513));
#175822=CARTESIAN_POINT('Ctrl Pts',(17.6160462231313,-17.1542602099344,
10.4401662187822));
#175823=CARTESIAN_POINT('Ctrl Pts',(17.6777425470872,-17.1158933457383,
10.4445479148834));
#175824=CARTESIAN_POINT('Ctrl Pts',(17.7415111977167,-17.0806471078961,
10.4489296109847));
#175825=CARTESIAN_POINT('Ctrl Pts',(17.8070029012401,-17.0487487346935,
10.453311307086));
#175826=CARTESIAN_POINT('Ctrl Pts',(17.8724176467997,-17.0168878446181,
10.4576878543456));
#175827=CARTESIAN_POINT('Ctrl Pts',(17.9395509916045,-16.9883672144276,
10.4620644016053));
#175828=CARTESIAN_POINT('Ctrl Pts',(18.0080275301105,-16.9633690707015,
10.4664409488649));
#175829=CARTESIAN_POINT('Ctrl Pts',(18.0764606417909,-16.9383867804349,
10.4708147205819));
#175830=CARTESIAN_POINT('Ctrl Pts',(18.1462348050105,-16.9169227092787,
10.4751884922988));
#175831=CARTESIAN_POINT('Ctrl Pts',(18.2169543269192,-16.8991111155378,
10.4795622640158));
#175832=CARTESIAN_POINT('Ctrl Pts',(18.2876523286398,-16.8813049419247,
10.4839347047794));
#175833=CARTESIAN_POINT('Ctrl Pts',(18.359294650436,-16.8671491568768,10.4883071455429));
#175834=CARTESIAN_POINT('Ctrl Pts',(18.4314717388387,-16.8567277858954,
10.4926795863064));
#175835=CARTESIAN_POINT('Ctrl Pts',(18.5036506728176,-16.8463061484384,
10.4970521388738));
#175836=CARTESIAN_POINT('Ctrl Pts',(18.5763639228391,-16.8396191815878,
10.5014246914411));
#175837=CARTESIAN_POINT('Ctrl Pts',(18.6491947479436,-16.8366992957918,
10.5057972440085));
#175838=CARTESIAN_POINT('Ctrl Pts',(18.7221011596255,-16.8337763796282,
10.5101743345758));
#175839=CARTESIAN_POINT('Ctrl Pts',(18.7951249069977,-16.8346283697016,
10.5145514251431));
#175840=CARTESIAN_POINT('Ctrl Pts',(18.8678480060379,-16.8392355286782,
10.5189285157104));
#175841=CARTESIAN_POINT('Ctrl Pts',(18.9406108218616,-16.8438452037953,
10.5233079967694));
#175842=CARTESIAN_POINT('Ctrl Pts',(19.0130721829178,-16.8522140756297,
10.5276874778283));
#175843=CARTESIAN_POINT('Ctrl Pts',(19.0848207051463,-16.8642706514396,
10.5320669588873));
#175844=CARTESIAN_POINT('Ctrl Pts',(19.156696401149,-16.8763485974491,10.536454202547));
#175845=CARTESIAN_POINT('Ctrl Pts',(19.2278562638074,-16.8921271959049,
10.5408414462067));
#175846=CARTESIAN_POINT('Ctrl Pts',(19.2979011262236,-16.911484251508,10.5452286898664));
#175847=CARTESIAN_POINT('Ctrl Pts',(19.3455248831598,-16.9246451840768,
10.5482115928012));
#175848=CARTESIAN_POINT('Ctrl Pts',(19.3926335158209,-16.9394592758343,
10.5511944957361));
#175849=CARTESIAN_POINT('Ctrl Pts',(19.4391069833084,-16.9558754692931,
10.5541773986709));
#175850=CARTESIAN_POINT('Ctrl Pts',(19.507475042724,-16.9800256640268,10.5585656076018));
#175851=CARTESIAN_POINT('Ctrl Pts',(19.5747343896099,-17.0077395128395,
10.5629538165327));
#175852=CARTESIAN_POINT('Ctrl Pts',(19.6404874892068,-17.0388953421437,
10.5673420254636));
#175853=CARTESIAN_POINT('Ctrl Pts',(19.7061430003017,-17.0700049310314,
10.5717237215648));
#175854=CARTESIAN_POINT('Ctrl Pts',(19.7702962696065,-17.1045461545567,
10.5761054176661));
#175855=CARTESIAN_POINT('Ctrl Pts',(19.8325671704115,-17.1423483285189,
10.5804871137674));
#175856=CARTESIAN_POINT('Ctrl Pts',(19.8947648979524,-17.1801060819184,
10.584863661027));
#175857=CARTESIAN_POINT('Ctrl Pts',(19.9550842407134,-17.2211169246315,
10.5892402082867));
#175858=CARTESIAN_POINT('Ctrl Pts',(20.013168775078,-17.2651638357963,10.5936167555463));
#175859=CARTESIAN_POINT('Ctrl Pts',(20.071216473075,-17.3091828130501,10.5979905272633));
#175860=CARTESIAN_POINT('Ctrl Pts',(20.1270317913336,-17.3562337476985,
10.6023642989803));
#175861=CARTESIAN_POINT('Ctrl Pts',(20.1802876588313,-17.4060565961484,
10.6067380706972));
#175862=CARTESIAN_POINT('Ctrl Pts',(20.2335273203896,-17.4558642833382,
10.6111105114608));
#175863=CARTESIAN_POINT('Ctrl Pts',(20.2842087253976,-17.5084418803649,
10.6154829522244));
#175864=CARTESIAN_POINT('Ctrl Pts',(20.332039538181,-17.5634904989845,10.6198553929879));
#175865=CARTESIAN_POINT('Ctrl Pts',(20.3798715740035,-17.6185405252034,
10.6242279455553));
#175866=CARTESIAN_POINT('Ctrl Pts',(20.4248525580102,-17.6760613330223,
10.6286004981226));
#175867=CARTESIAN_POINT('Ctrl Pts',(20.4667296641659,-17.735720052406,10.63297305069));
#175868=CARTESIAN_POINT('Ctrl Pts',(20.508650231962,-17.7954406878589,10.6373501412573));
#175869=CARTESIAN_POINT('Ctrl Pts',(20.5474602125883,-17.8573032692078,
10.6417272318246));
#175870=CARTESIAN_POINT('Ctrl Pts',(20.5829499551955,-17.920945654593,10.646104322392));
#175871=CARTESIAN_POINT('Ctrl Pts',(20.6184590800684,-17.984622797447,10.6504838034509));
#175872=CARTESIAN_POINT('Ctrl Pts',(20.6506441436597,-18.0500812464321,
10.6548632845098));
#175873=CARTESIAN_POINT('Ctrl Pts',(20.679342585662,-18.1169363949915,10.6592427655688));
#175874=CARTESIAN_POINT('Ctrl Pts',(20.7080918954602,-18.1839100438528,
10.6636300092285));
#175875=CARTESIAN_POINT('Ctrl Pts',(20.7333420751797,-18.2522848831355,
10.6680172528882));
#175876=CARTESIAN_POINT('Ctrl Pts',(20.7549798102579,-18.3216591346502,
10.672404496548));
#175877=CARTESIAN_POINT('Ctrl Pts',(20.7696913851038,-18.368826940793,10.6753873994828));
#175878=CARTESIAN_POINT('Ctrl Pts',(20.7827340876901,-18.4164564326549,
10.6783703024176));
#175879=CARTESIAN_POINT('Ctrl Pts',(20.794085873422,-18.4644190383875,10.6813532053524));
#175880=CARTESIAN_POINT('Ctrl Pts',(20.8107857153611,-18.5349777992406,
10.6857414142833));
#175881=CARTESIAN_POINT('Ctrl Pts',(20.8238889631161,-18.6065332466769,
10.6901296232142));
#175882=CARTESIAN_POINT('Ctrl Pts',(20.8332827468939,-18.6786852572696,
10.6945178321451));
#175883=CARTESIAN_POINT('Ctrl Pts',(20.8426625887389,-18.7507301823154,
10.6988995282463));
#175884=CARTESIAN_POINT('Ctrl Pts',(20.8483438339329,-18.8233694384939,
10.7032812243476));
#175885=CARTESIAN_POINT('Ctrl Pts',(20.8502642454991,-18.896191011278,10.7076629204489));
#175886=CARTESIAN_POINT('Ctrl Pts',(20.8521824004289,-18.9689270129188,
10.7120394677085));
#175887=CARTESIAN_POINT('Ctrl Pts',(20.8503484880034,-19.0418444257663,
10.7164160149681));
#175888=CARTESIAN_POINT('Ctrl Pts',(20.8447520630799,-19.1145260846878,
10.7207925622278));
#175889=CARTESIAN_POINT('Ctrl Pts',(20.8391591873278,-19.1871616499575,
10.7251663339448));
#175890=CARTESIAN_POINT('Ctrl Pts',(20.8298085704124,-19.2595612781811,
10.7295401056617));
#175891=CARTESIAN_POINT('Ctrl Pts',(20.8167418305018,-19.3313091977237,
10.7339138773787));
#175892=CARTESIAN_POINT('Ctrl Pts',(20.8036790668441,-19.4030352841335,
10.7382863181423));
#175893=CARTESIAN_POINT('Ctrl Pts',(20.7869025116117,-19.4741095812966,
10.7426587589058));
#175894=CARTESIAN_POINT('Ctrl Pts',(20.7665052467619,-19.5441244986363,
10.7470311996694));
#175895=CARTESIAN_POINT('Ctrl Pts',(20.7461074603518,-19.6141412062652,
10.7514037522367));
#175896=CARTESIAN_POINT('Ctrl Pts',(20.7220889173522,-19.6830980177239,
10.755776304804));
#175897=CARTESIAN_POINT('Ctrl Pts',(20.6945926588476,-19.7506021700904,
10.7601488573714));
#175898=CARTESIAN_POINT('Ctrl Pts',(20.6670678636887,-19.8181763808124,
10.7645259479387));
#175899=CARTESIAN_POINT('Ctrl Pts',(20.6360583291635,-19.884294474674,10.768903038506));
#175900=CARTESIAN_POINT('Ctrl Pts',(20.6017550792374,-19.9485841479688,
10.7732801290734));
#175901=CARTESIAN_POINT('Ctrl Pts',(20.5674330950334,-20.0129089322404,
10.7776596101323));
#175902=CARTESIAN_POINT('Ctrl Pts',(20.5298140629451,-20.0754028942418,
10.7820390911912));
#175903=CARTESIAN_POINT('Ctrl Pts',(20.4891333854102,-20.1357211662458,
10.7864185722502));
#175904=CARTESIAN_POINT('Ctrl Pts',(20.4483806016475,-20.1961463519821,
10.7908058159099));
#175905=CARTESIAN_POINT('Ctrl Pts',(20.4045556257384,-20.2543877608709,
10.7951930595696));
#175906=CARTESIAN_POINT('Ctrl Pts',(20.3579349545336,-20.310132638384,10.7995803032293));
#175907=CARTESIAN_POINT('Ctrl Pts',(20.3262373904716,-20.3480337835292,
10.8025632061641));
#175908=CARTESIAN_POINT('Ctrl Pts',(20.2932482928817,-20.384781572932,10.8055461090989));
#175909=CARTESIAN_POINT('Ctrl Pts',(20.2590638380205,-20.4202878770739,
10.8085290120338));
#175910=CARTESIAN_POINT('Ctrl Pts',(20.208774394013,-20.4725219203344,10.8129172209647));
#175911=CARTESIAN_POINT('Ctrl Pts',(20.1557001261013,-20.5222712846033,
10.8173054298956));
#175912=CARTESIAN_POINT('Ctrl Pts',(20.1001163804877,-20.5692244850246,
10.8216936388265));
#175913=CARTESIAN_POINT('Ctrl Pts',(20.0446151303687,-20.6161079991114,
10.8260753349277));
#175914=CARTESIAN_POINT('Ctrl Pts',(19.9866121616043,-20.6602032788999,
10.830457031029));
#175915=CARTESIAN_POINT('Ctrl Pts',(19.9264202255139,-20.7012349772931,
10.8348387271302));
#175916=CARTESIAN_POINT('Ctrl Pts',(19.8662990197386,-20.7422184601752,
10.8392152743899));
#175917=CARTESIAN_POINT('Ctrl Pts',(19.8039943529516,-20.7801452426345,
10.8435918216495));
#175918=CARTESIAN_POINT('Ctrl Pts',(19.739851341254,-20.8147807383848,10.8479683689092));
#175919=CARTESIAN_POINT('Ctrl Pts',(19.6757490081222,-20.8493942688071,
10.8523421406261));
#175920=CARTESIAN_POINT('Ctrl Pts',(19.6098110666879,-20.8807204253384,
10.8567159123431));
#175921=CARTESIAN_POINT('Ctrl Pts',(19.5424096422237,-20.9085691529715,
10.8610896840601));
#175922=CARTESIAN_POINT('Ctrl Pts',(19.4750287282393,-20.9364094061433,
10.8654621248236));
#175923=CARTESIAN_POINT('Ctrl Pts',(19.4061856609217,-20.9607741471641,
10.8698345655872));
#175924=CARTESIAN_POINT('Ctrl Pts',(19.3362735429414,-20.9815210221806,
10.8742070063508));
#175925=CARTESIAN_POINT('Ctrl Pts',(19.2663596373003,-21.002268427697,10.8785795589181));
#175926=CARTESIAN_POINT('Ctrl Pts',(19.1953770897375,-21.0193976482244,
10.8829521114855));
#175927=CARTESIAN_POINT('Ctrl Pts',(19.1237335771401,-21.0328163635577,
10.8873246640528));
#175928=CARTESIAN_POINT('Ctrl Pts',(19.0520157102031,-21.0462490053399,
10.8917017546201));
#175929=CARTESIAN_POINT('Ctrl Pts',(18.9796359837846,-21.0559633643479,
10.8960788451875));
#175930=CARTESIAN_POINT('Ctrl Pts',(18.9070108440327,-21.0619185405714,
10.9004559357548));
#175931=CARTESIAN_POINT('Ctrl Pts',(18.8343460409964,-21.0678769691378,
10.9048354168137));
#175932=CARTESIAN_POINT('Ctrl Pts',(18.7614360402691,-21.070072112832,10.9092148978727));
#175933=CARTESIAN_POINT('Ctrl Pts',(18.6886982399077,-21.0685152374912,
10.9135943789316));
#175934=CARTESIAN_POINT('Ctrl Pts',(18.6158315122834,-21.0669556025994,
10.9179816225913));
#175935=CARTESIAN_POINT('Ctrl Pts',(18.5431380760574,-21.0616307033084,
10.9223688662511));
#175936=CARTESIAN_POINT('Ctrl Pts',(18.4710305707949,-21.0526037416189,
10.9267561099108));
#175937=CARTESIAN_POINT('Ctrl Pts',(18.4220044154792,-21.0464662775061,
10.9297390128456));
#175938=CARTESIAN_POINT('Ctrl Pts',(18.3732489672178,-21.0386185484977,
10.9327219157804));
#175939=CARTESIAN_POINT('Ctrl Pts',(18.3248903873721,-21.0290937207684,
10.9357048187152));
#175940=CARTESIAN_POINT('Ctrl Pts',(18.2537491009802,-21.0150815537551,
10.9400930276461));
#175941=CARTESIAN_POINT('Ctrl Pts',(18.1831896640503,-20.9973828809338,
10.944481236577));
#175942=CARTESIAN_POINT('Ctrl Pts',(18.1136230257297,-20.9760606240415,
10.9488694455079));
#175943=CARTESIAN_POINT('Ctrl Pts',(18.0441596358346,-20.9547700129136,
10.9532511416091));
#175944=CARTESIAN_POINT('Ctrl Pts',(17.9756865768829,-20.929866633968,10.9576328377104));
#175945=CARTESIAN_POINT('Ctrl Pts',(17.9086046585659,-20.9014644214088,
10.9620145338117));
#175946=CARTESIAN_POINT('Ctrl Pts',(17.8416015668415,-20.8730955837098,
10.9663910810713));
#175947=CARTESIAN_POINT('Ctrl Pts',(17.7759868104063,-20.8412362668761,
10.970767628331));
#175948=CARTESIAN_POINT('Ctrl Pts',(17.7121444440029,-20.8060496818256,
10.9751441755906));
#175949=CARTESIAN_POINT('Ctrl Pts',(17.6483425655005,-20.7708854115961,
10.9795179473076));
#175950=CARTESIAN_POINT('Ctrl Pts',(17.5863112682431,-20.7323982921383,
10.9838917190245));
#175951=CARTESIAN_POINT('Ctrl Pts',(17.5264117827671,-20.6907983487456,
10.9882654907415));
#175952=CARTESIAN_POINT('Ctrl Pts',(17.4665305249056,-20.6492110643553,
10.9926379315051));
#175953=CARTESIAN_POINT('Ctrl Pts',(17.4087801868841,-20.6045131115935,
10.9970103722686));
#175954=CARTESIAN_POINT('Ctrl Pts',(17.3534932447848,-20.5569579741555,
11.0013828130322));
#175955=CARTESIAN_POINT('Ctrl Pts',(17.2982048889925,-20.5094016207274,
11.0057553655995));
#175956=CARTESIAN_POINT('Ctrl Pts',(17.2453804185818,-20.4589882536492,
11.0101279181668));
#175957=CARTESIAN_POINT('Ctrl Pts',(17.1953181280021,-20.4060106934906,
11.0145004707342));
#175958=CARTESIAN_POINT('Ctrl Pts',(17.1452038808888,-20.3529781512217,
11.0188775613015));
#175959=CARTESIAN_POINT('Ctrl Pts',(17.0978578691735,-20.2973764539274,
11.0232546518688));
#175960=CARTESIAN_POINT('Ctrl Pts',(17.0535398976935,-20.2395336285146,
11.0276317424362));
#175961=CARTESIAN_POINT('Ctrl Pts',(17.0091977225243,-20.1816592129879,
11.0320112234951));
#175962=CARTESIAN_POINT('Ctrl Pts',(16.9678871535202,-20.1215416302814,
11.036390704554));
#175963=CARTESIAN_POINT('Ctrl Pts',(16.9298246475467,-20.0595379440905,
11.040770185613));
#175964=CARTESIAN_POINT('Ctrl Pts',(16.8916946760369,-19.997424356782,11.0451574292727));
#175965=CARTESIAN_POINT('Ctrl Pts',(16.856824495368,-19.9334184139102,11.0495446729324));
#175966=CARTESIAN_POINT('Ctrl Pts',(16.8253843166295,-19.8679012900919,
11.0539319165921));
#175967=CARTESIAN_POINT('Ctrl Pts',(16.8040080246555,-19.8233559591102,
11.056914819527));
#175968=CARTESIAN_POINT('Ctrl Pts',(16.7842163233976,-19.7781125159704,
11.0598977224618));
#175969=CARTESIAN_POINT('Ctrl Pts',(16.7660496141036,-19.7322949946336,
11.0628806253966));
#175970=CARTESIAN_POINT('Ctrl Pts',(16.7358636223541,-19.6561641280759,
11.0678370477142));
#175971=CARTESIAN_POINT('Ctrl Pts',(16.7100671742202,-19.578198920716,11.0727934700317));
#175972=CARTESIAN_POINT('Ctrl Pts',(16.6888585600969,-19.4988870914467,
11.0777498923492));
#175973=CARTESIAN_POINT('Ctrl Pts',(16.6677318984788,-19.4198817321365,
11.0826871624852));
#175974=CARTESIAN_POINT('Ctrl Pts',(16.6511578246449,-19.3395403557194,
11.0876244326213));
#175975=CARTESIAN_POINT('Ctrl Pts',(16.6392856441441,-19.2583670468102,
11.0925617027573));
#175976=CARTESIAN_POINT('Ctrl Pts',(16.6274900435723,-19.1777173355868,
11.0974671256858));
#175977=CARTESIAN_POINT('Ctrl Pts',(16.6203359927508,-19.0962466252342,
11.1023725486143));
#175978=CARTESIAN_POINT('Ctrl Pts',(16.6179218376289,-19.0144676775316,
11.1072779715428));
#175979=CARTESIAN_POINT('Ctrl Pts',(16.6173204835912,-18.9940969482629,
11.1084998880046));
#175980=CARTESIAN_POINT('Ctrl Pts',(16.6170129926863,-18.9737071731887,
11.1097218044664));
#175981=CARTESIAN_POINT('Ctrl Pts',(16.6170004031077,-18.9533064294667,
11.1109437209282));
#175982=CARTESIAN_POINT('',(16.6170004031077,-18.9506935705328,10.8890562790718));
#175983=CARTESIAN_POINT('Ctrl Pts',(16.7454193829761,-18.2258897262833,
10.1325348909312));
#175984=CARTESIAN_POINT('Ctrl Pts',(16.7957300955987,-18.0881049963718,
10.1420538200687));
#175985=CARTESIAN_POINT('Ctrl Pts',(16.8602294232363,-17.9559072036814,
10.1518904229148));
#175986=CARTESIAN_POINT('Ctrl Pts',(16.9705620789177,-17.7790615297577,
10.1654299256796));
#175987=CARTESIAN_POINT('Ctrl Pts',(17.0055077313234,-17.7281479046147,
10.1693725844016));
#175988=CARTESIAN_POINT('Ctrl Pts',(17.0481243243609,-17.6715330475318,
10.1737463481034));
#175989=CARTESIAN_POINT('Ctrl Pts',(17.0536641597985,-17.6642718139689,
10.1743070933956));
#175990=CARTESIAN_POINT('Ctrl Pts',(17.0620088150317,-17.6534797633357,
10.175139888946));
#175991=CARTESIAN_POINT('Ctrl Pts',(17.064778120803,-17.6499217970805,10.1754143473587));
#175992=CARTESIAN_POINT('Ctrl Pts',(17.0697578837249,-17.6435658623637,
10.1759044156734));
#175993=CARTESIAN_POINT('Ctrl Pts',(17.0719640541656,-17.6407646170597,
10.1761203224753));
#175994=CARTESIAN_POINT('Ctrl Pts',(17.0767598422769,-17.6347068017437,
10.1765870501452));
#175995=CARTESIAN_POINT('Ctrl Pts',(17.0793519775629,-17.6314522980704,
10.1768376869375));
#175996=CARTESIAN_POINT('Ctrl Pts',(17.0866262035549,-17.6223743351843,
10.177536565398));
#175997=CARTESIAN_POINT('Ctrl Pts',(17.0913296095108,-17.61656792545,10.1779833059919));
#175998=CARTESIAN_POINT('Ctrl Pts',(17.1189523502469,-17.5828340816282,
10.1805779702704));
#175999=CARTESIAN_POINT('Ctrl Pts',(17.1425543086516,-17.555470306126,10.182679512319));
#176000=CARTESIAN_POINT('Ctrl Pts',(17.2209746894621,-17.469122602259,10.1893509058033));
#176001=CARTESIAN_POINT('Ctrl Pts',(17.2784630223073,-17.41265432694,10.1937780093484));
#176002=CARTESIAN_POINT('Ctrl Pts',(17.4407098117256,-17.2705240626054,
10.205535089745));
#176003=CARTESIAN_POINT('Ctrl Pts',(17.550678297492,-17.1914009901979,10.2127865843535));
#176004=CARTESIAN_POINT('Ctrl Pts',(17.7219085497416,-17.0915333198103,
10.223936955663));
#176005=CARTESIAN_POINT('Ctrl Pts',(17.7777672580292,-17.0622160944038,
10.2275505927027));
#176006=CARTESIAN_POINT('Ctrl Pts',(17.8461537358047,-17.0301326842564,
10.2319867407696));
#176007=CARTESIAN_POINT('Ctrl Pts',(17.8575065578041,-17.0249285939676,
10.2327235176444));
#176008=CARTESIAN_POINT('Ctrl Pts',(17.8762116742383,-17.0165537245252,
10.2339382828108));
#176009=CARTESIAN_POINT('Ctrl Pts',(17.8835371883593,-17.0133236215431,
10.2344142317329));
#176010=CARTESIAN_POINT('Ctrl Pts',(17.8967322480422,-17.0075945880762,
10.23527198129));
#176011=CARTESIAN_POINT('Ctrl Pts',(17.9025951268876,-17.0050804767594,
10.2356532576554));
#176012=CARTESIAN_POINT('Ctrl Pts',(17.915097202723,-16.9997861242286,10.2364666714788));
#176013=CARTESIAN_POINT('Ctrl Pts',(17.9217393818782,-16.9970131728325,
10.2368990510978));
#176014=CARTESIAN_POINT('Ctrl Pts',(17.9396436277685,-16.9896455727855,
10.2380652135793));
#176015=CARTESIAN_POINT('Ctrl Pts',(17.9509312379949,-16.985114073362,10.2388011205731));
#176016=CARTESIAN_POINT('Ctrl Pts',(18.0072714631114,-16.9630576984454,
10.2424782702486));
#176017=CARTESIAN_POINT('Ctrl Pts',(18.0528730393969,-16.9469834640486,
10.2454676595449));
#176018=CARTESIAN_POINT('Ctrl Pts',(18.1854403760795,-16.9052988818691,
10.2542017471225));
#176019=CARTESIAN_POINT('Ctrl Pts',(18.2735461488255,-16.883695804691,10.2600638157415));
#176020=CARTESIAN_POINT('Ctrl Pts',(18.5213291246805,-16.8395598987305,
10.2765863302488));
#176021=CARTESIAN_POINT('Ctrl Pts',(18.6826103942637,-16.8295026002585,
10.2874126707951));
#176022=CARTESIAN_POINT('Ctrl Pts',(18.8634558574733,-16.8388671481655,
10.2987727144306));
#176023=CARTESIAN_POINT('Ctrl Pts',(18.883420982029,-16.8401849735893,10.3000154305921));
#176024=CARTESIAN_POINT('Ctrl Pts',(18.9097266868776,-16.8422962624498,
10.3016351183705));
#176025=CARTESIAN_POINT('Ctrl Pts',(18.9160858892075,-16.8428356014584,
10.3020252987239));
#176026=CARTESIAN_POINT('Ctrl Pts',(18.9263462769461,-16.8437525596449,
10.3026525301919));
#176027=CARTESIAN_POINT('Ctrl Pts',(18.9302489657443,-16.8441122648393,
10.3028905662142));
#176028=CARTESIAN_POINT('Ctrl Pts',(18.9377548121748,-16.8448250942274,
10.3033472991222));
#176029=CARTESIAN_POINT('Ctrl Pts',(18.9413580661832,-16.8451766235564,
10.3035660799459));
#176030=CARTESIAN_POINT('Ctrl Pts',(18.9498804195589,-16.8460301299421,
10.3040824355745));
#176031=CARTESIAN_POINT('Ctrl Pts',(18.9547987304329,-16.8465401046539,
10.3043795614182));
#176032=CARTESIAN_POINT('Ctrl Pts',(18.9711072085082,-16.8482888885894,
10.3053620494374));
#176033=CARTESIAN_POINT('Ctrl Pts',(18.9824893314753,-16.8496029552277,
10.306043313592));
#176034=CARTESIAN_POINT('Ctrl Pts',(19.0908934098305,-16.8630108870786,
10.3124941111033));
#176035=CARTESIAN_POINT('Ctrl Pts',(19.1869913741393,-16.8817217354081,
10.3179276581124));
#176036=CARTESIAN_POINT('Ctrl Pts',(19.3427049008834,-16.9234076637989,
10.3267475068387));
#176037=CARTESIAN_POINT('Ctrl Pts',(19.4031811908957,-16.9425460341899,
10.3301766235674));
#176038=CARTESIAN_POINT('Ctrl Pts',(19.598052165044,-17.0139899175417,10.3414650180681));
#176039=CARTESIAN_POINT('Ctrl Pts',(19.7279547876522,-17.0772959386383,
10.3494033927115));
#176040=CARTESIAN_POINT('Ctrl Pts',(19.8625423237699,-17.1608313634513,
10.3586834022296));
#176041=CARTESIAN_POINT('Ctrl Pts',(19.8745968344252,-17.1684833313024,
10.3595242186359));
#176042=CARTESIAN_POINT('Ctrl Pts',(19.8936617334745,-17.1808576884849,
10.3608698985987));
#176043=CARTESIAN_POINT('Ctrl Pts',(19.9007229663745,-17.1855012198422,
10.3613718271763));
#176044=CARTESIAN_POINT('Ctrl Pts',(19.9131291707898,-17.1937664882229,
10.362260004276));
#176045=CARTESIAN_POINT('Ctrl Pts',(19.9184857630501,-17.1973706490971,
10.3626455879037));
#176046=CARTESIAN_POINT('Ctrl Pts',(19.9295324842425,-17.2048770268249,
10.363445158131));
#176047=CARTESIAN_POINT('Ctrl Pts',(19.9352201842589,-17.2087826666043,
10.3638592716852));
#176048=CARTESIAN_POINT('Ctrl Pts',(19.9497743039565,-17.2188817658624,
10.3649252613995));
#176049=CARTESIAN_POINT('Ctrl Pts',(19.9586124573843,-17.2251154369552,
10.3655786697191));
#176050=CARTESIAN_POINT('Ctrl Pts',(19.9953313402991,-17.2514374114025,
10.3683191174326));
#176051=CARTESIAN_POINT('Ctrl Pts',(20.0227673488513,-17.2721344188028,
10.3704295818428));
#176052=CARTESIAN_POINT('Ctrl Pts',(20.0929585128365,-17.3278166276143,
10.3759988928031));
#176053=CARTESIAN_POINT('Ctrl Pts',(20.1348674597177,-17.363821987084,10.3794963808924));
#176054=CARTESIAN_POINT('Ctrl Pts',(20.2555226388132,-17.4759753460129,
10.3900858946476));
#176055=CARTESIAN_POINT('Ctrl Pts',(20.3298163930958,-17.5566339203428,
10.3973262438312));
#176056=CARTESIAN_POINT('Ctrl Pts',(20.4322357464445,-17.6867598286241,
10.4082648890072));
#176057=CARTESIAN_POINT('Ctrl Pts',(20.4651734761693,-17.7322147127585,
10.4119625540102));
#176058=CARTESIAN_POINT('Ctrl Pts',(20.5072149341785,-17.7953720873743,
10.4168929756721));
#176059=CARTESIAN_POINT('Ctrl Pts',(20.5179321087802,-17.8119712278225,
10.4181702261452));
#176060=CARTESIAN_POINT('Ctrl Pts',(20.5517785990921,-17.8660401880973,
10.4222657511306));
#176061=CARTESIAN_POINT('Ctrl Pts',(20.5739734608864,-17.9040849126947,
10.4250486655385));
#176062=CARTESIAN_POINT('Ctrl Pts',(20.5985622110295,-17.9494264940757,
10.4282277276706));
#176063=CARTESIAN_POINT('Ctrl Pts',(20.6021219391083,-17.9560751543949,
10.4286904986772));
#176064=CARTESIAN_POINT('Ctrl Pts',(20.6077880740002,-17.9667953184576,
10.4294310513469));
#176065=CARTESIAN_POINT('Ctrl Pts',(20.6099168813717,-17.9708548191551,
10.4297101978003));
#176066=CARTESIAN_POINT('Ctrl Pts',(20.613684915443,-17.9780973167066,10.4302058901149));
#176067=CARTESIAN_POINT('Ctrl Pts',(20.6153292700714,-17.9812775905825,
10.4304227568122));
#176068=CARTESIAN_POINT('Ctrl Pts',(20.6188210100783,-17.9880730103868,
10.4308844322552));
#176069=CARTESIAN_POINT('Ctrl Pts',(20.6206660621078,-17.9916892939962,
10.4311290944162));
#176070=CARTESIAN_POINT('Ctrl Pts',(20.6256700598912,-18.0015671669466,
10.4317946569639));
#176071=CARTESIAN_POINT('Ctrl Pts',(20.6288083440272,-18.0078392466441,
10.4322142797877));
#176072=CARTESIAN_POINT('Ctrl Pts',(20.6449306666892,-18.0404649883131,
10.4343821965714));
#176073=CARTESIAN_POINT('Ctrl Pts',(20.6573969642439,-18.0670726556243,
10.4361001290225));
#176074=CARTESIAN_POINT('Ctrl Pts',(20.6927930372405,-18.1469058250094,
10.4411321133958));
#176075=CARTESIAN_POINT('Ctrl Pts',(20.7140968879184,-18.2008248804714,
10.4443722525155));
#176076=CARTESIAN_POINT('Ctrl Pts',(20.7880001367405,-18.4129655902131,
10.4567569627002));
#176077=CARTESIAN_POINT('Ctrl Pts',(20.8240537212191,-18.5762984991833,
10.4655773723993));
#176078=CARTESIAN_POINT('Ctrl Pts',(20.8467111687562,-18.8037693452038,
10.4784462498715));
#176079=CARTESIAN_POINT('Ctrl Pts',(20.8501415170503,-18.8656006986345,
10.481995657321));
#176080=CARTESIAN_POINT('Ctrl Pts',(20.851001813363,-18.9399010419642,10.4863598615508));
#176081=CARTESIAN_POINT('Ctrl Pts',(20.8510363611967,-18.9523132244191,
10.4870921832702));
#176082=CARTESIAN_POINT('Ctrl Pts',(20.8509137753343,-18.9727072276153,
10.4883010838398));
#176083=CARTESIAN_POINT('Ctrl Pts',(20.8508206458101,-18.9806892362942,
10.4887756571352));
#176084=CARTESIAN_POINT('Ctrl Pts',(20.8505719131426,-18.9950465220383,
10.4896319060536));
#176085=CARTESIAN_POINT('Ctrl Pts',(20.8504326424018,-19.0014220129529,
10.4900130651295));
#176086=CARTESIAN_POINT('Ctrl Pts',(20.8500744597129,-19.0150072072234,
10.4908272862738));
#176087=CARTESIAN_POINT('Ctrl Pts',(20.8498475025669,-19.0222166012236,
10.4912605959793));
#176088=CARTESIAN_POINT('Ctrl Pts',(20.8491363508173,-19.0416484168717,
10.4924318670969));
#176089=CARTESIAN_POINT('Ctrl Pts',(20.8485830661029,-19.0538678943721,
10.4931719848728));
#176090=CARTESIAN_POINT('Ctrl Pts',(20.84527274177,-19.1152079183555,10.4969057361948));
#176091=CARTESIAN_POINT('Ctrl Pts',(20.8409100773936,-19.1642232531996,
10.4999493174715));
#176092=CARTESIAN_POINT('Ctrl Pts',(20.8233582365969,-19.3054805611817,
10.5089013130598));
#176093=CARTESIAN_POINT('Ctrl Pts',(20.8057844131461,-19.3970531799347,
10.5149344377632));
#176094=CARTESIAN_POINT('Ctrl Pts',(20.7404394493395,-19.6471496014099,
10.5319198922653));
#176095=CARTESIAN_POINT('Ctrl Pts',(20.68003645299,-19.8016941123581,10.5430358164807));
#176096=CARTESIAN_POINT('Ctrl Pts',(20.5956714639142,-19.9600002883786,
10.5541994886098));
#176097=CARTESIAN_POINT('Ctrl Pts',(20.5889607295882,-19.9722969844839,
10.5550647355217));
#176098=CARTESIAN_POINT('Ctrl Pts',(20.5794327277478,-19.9893512379545,
10.5562611083863));
#176099=CARTESIAN_POINT('Ctrl Pts',(20.5767183061933,-19.9941654327063,
10.5565984207689));
#176100=CARTESIAN_POINT('Ctrl Pts',(20.5723233068981,-20.0018893795181,
10.5571388818417));
#176101=CARTESIAN_POINT('Ctrl Pts',(20.5706546217147,-20.0048058181875,
10.5573427838927));
#176102=CARTESIAN_POINT('Ctrl Pts',(20.5671475192382,-20.0109016293311,
10.5577685998503));
#176103=CARTESIAN_POINT('Ctrl Pts',(20.5653077651162,-20.0140802029747,
10.557990421151));
#176104=CARTESIAN_POINT('Ctrl Pts',(20.56082543039,-20.021778133228,10.558527149732));
#176105=CARTESIAN_POINT('Ctrl Pts',(20.5581743168869,-20.0262925441416,
10.5588415070615));
#176106=CARTESIAN_POINT('Ctrl Pts',(20.548779785926,-20.0421548395615,10.5599448062051));
#176107=CARTESIAN_POINT('Ctrl Pts',(20.5419468468524,-20.0534497103275,
10.5607281413541));
#176108=CARTESIAN_POINT('Ctrl Pts',(20.500501331558,-20.1205343252392,10.5653715579759));
#176109=CARTESIAN_POINT('Ctrl Pts',(20.4634110576857,-20.1747585579245,
10.5690872775558));
#176110=CARTESIAN_POINT('Ctrl Pts',(20.3658366028335,-20.3040637622089,
10.5780787822703));
#176111=CARTESIAN_POINT('Ctrl Pts',(20.3026344321485,-20.3769051043167,
10.58326573562));
#176112=CARTESIAN_POINT('Ctrl Pts',(20.1353215694684,-20.5450581279599,
10.596173804659));
#176113=CARTESIAN_POINT('Ctrl Pts',(20.0262483793294,-20.6347426860893,
10.6039450996367));
#176114=CARTESIAN_POINT('Ctrl Pts',(19.8972047642764,-20.7208549094597,
10.6130336388409));
#176115=CARTESIAN_POINT('Ctrl Pts',(19.8852441157579,-20.7286625975121,
10.6138747668989));
#176116=CARTESIAN_POINT('Ctrl Pts',(19.8660809969454,-20.7408971648408,
10.6152208524136));
#176117=CARTESIAN_POINT('Ctrl Pts',(19.8589293061762,-20.7454030508966,
10.6157228720888));
#176118=CARTESIAN_POINT('Ctrl Pts',(19.8462676904791,-20.7532749016597,
10.6166111552809));
#176119=CARTESIAN_POINT('Ctrl Pts',(19.8407689618323,-20.7566587351442,
10.6169967533925));
#176120=CARTESIAN_POINT('Ctrl Pts',(19.8293628577293,-20.763606139712,10.6177962995137));
#176121=CARTESIAN_POINT('Ctrl Pts',(19.8234533765537,-20.7671660899483,
10.6182103742107));
#176122=CARTESIAN_POINT('Ctrl Pts',(19.8082377604992,-20.7762311101344,
10.6192761497955));
#176123=CARTESIAN_POINT('Ctrl Pts',(19.7989067446197,-20.7816938344257,
10.619929381656));
#176124=CARTESIAN_POINT('Ctrl Pts',(19.7597685938769,-20.8042059637299,
10.6226681172258));
#176125=CARTESIAN_POINT('Ctrl Pts',(19.7295920764681,-20.8205995666826,
10.6247770093685));
#176126=CARTESIAN_POINT('Ctrl Pts',(19.6499190661354,-20.8614046162073,
10.6303411813431));
#176127=CARTESIAN_POINT('Ctrl Pts',(19.599845617929,-20.8846262613374,10.6338350138812));
#176128=CARTESIAN_POINT('Ctrl Pts',(19.4479034434923,-20.9479989179057,
10.6444175085463));
#176129=CARTESIAN_POINT('Ctrl Pts',(19.343772485754,-20.9822324641211,10.6516545180829));
#176130=CARTESIAN_POINT('Ctrl Pts',(19.1859148345377,-21.0208836174798,
10.6623900390253));
#176131=CARTESIAN_POINT('Ctrl Pts',(19.1339001047365,-21.0315640599736,
10.665888562512));
#176132=CARTESIAN_POINT('Ctrl Pts',(19.0703147680502,-21.0421461233079,
10.6700841988521));
#176133=CARTESIAN_POINT('Ctrl Pts',(19.0590769322727,-21.0439233816769,
10.6708226466741));
#176134=CARTESIAN_POINT('Ctrl Pts',(18.9936910705494,-21.0537245048849,
10.6750995285825));
#176135=CARTESIAN_POINT('Ctrl Pts',(18.9392573580883,-21.0597371452283,
10.6785821640569));
#176136=CARTESIAN_POINT('Ctrl Pts',(18.8758953721517,-21.0642574858035,
10.6825011444287));
#176137=CARTESIAN_POINT('Ctrl Pts',(18.8671396493571,-21.064827447488,10.6830397054138));
#176138=CARTESIAN_POINT('Ctrl Pts',(18.8538934582752,-21.0656070499557,
10.683849701606));
#176139=CARTESIAN_POINT('Ctrl Pts',(18.8494055749012,-21.065856844042,10.6841233051208));
#176140=CARTESIAN_POINT('Ctrl Pts',(18.8413570849555,-21.0662791119787,
10.6846124554604));
#176141=CARTESIAN_POINT('Ctrl Pts',(18.8377968223099,-21.0664568870779,
10.6848282944198));
#176142=CARTESIAN_POINT('Ctrl Pts',(18.8300697887916,-21.06682315865,10.6852955705623));
#176143=CARTESIAN_POINT('Ctrl Pts',(18.8259029180993,-21.0670083335568,
10.6855468199258));
#176144=CARTESIAN_POINT('Ctrl Pts',(18.8142222737853,-21.0674928343694,
10.686249138739));
#176145=CARTESIAN_POINT('Ctrl Pts',(18.8067073264849,-21.0677644467195,
10.6866986831168));
#176146=CARTESIAN_POINT('Ctrl Pts',(18.7622839394637,-21.0691330709559,
10.6893433078396));
#176147=CARTESIAN_POINT('Ctrl Pts',(18.7253509201075,-21.0693044155801,
10.6914898955078));
#176148=CARTESIAN_POINT('Ctrl Pts',(18.6049318609852,-21.0667116984082,
10.6983731024294));
#176149=CARTESIAN_POINT('Ctrl Pts',(18.5216064838216,-21.0599742269612,
10.7029563517985));
#176150=CARTESIAN_POINT('Ctrl Pts',(18.2601185176632,-21.0231635594019,
10.7173370130993));
#176151=CARTESIAN_POINT('Ctrl Pts',(18.0853202367127,-20.9752375786342,
10.727017925168));
#176152=CARTESIAN_POINT('Ctrl Pts',(17.8978823138714,-20.8970208991988,
10.7388247297871));
#176153=CARTESIAN_POINT('Ctrl Pts',(17.8771803841266,-20.8879904884649,
10.7401482447523));
#176154=CARTESIAN_POINT('Ctrl Pts',(17.8480006649476,-20.8747022737725,
10.7420432804298));
#176155=CARTESIAN_POINT('Ctrl Pts',(17.8394004628251,-20.8707158515336,
10.7426054945982));
#176156=CARTESIAN_POINT('Ctrl Pts',(17.8254417699695,-20.8641313767579,
10.7435241416538));
#176157=CARTESIAN_POINT('Ctrl Pts',(17.8200668973459,-20.8615682082857,
10.7438793637465));
#176158=CARTESIAN_POINT('Ctrl Pts',(17.8089337632939,-20.8562012698316,
10.7446182815487));
#176159=CARTESIAN_POINT('Ctrl Pts',(17.8031772745161,-20.8533939809112,
10.7450020970094));
#176160=CARTESIAN_POINT('Ctrl Pts',(17.7895799502217,-20.846686375174,10.7459128997777));
#176161=CARTESIAN_POINT('Ctrl Pts',(17.7817504481549,-20.8427634643451,
10.7464406737091));
#176162=CARTESIAN_POINT('Ctrl Pts',(17.7651878395372,-20.834335930139,10.7475642902708));
#176163=CARTESIAN_POINT('Ctrl Pts',(17.7564613274093,-20.8298188662999,
10.7481605624398));
#176164=CARTESIAN_POINT('Ctrl Pts',(17.7328116850041,-20.8173676858811,
10.7497882722988));
#176165=CARTESIAN_POINT('Ctrl Pts',(17.7179518542265,-20.8093154780856,
10.750823855531));
#176166=CARTESIAN_POINT('Ctrl Pts',(17.6715974713707,-20.7834743140046,
10.7540953971307));
#176167=CARTESIAN_POINT('Ctrl Pts',(17.640462742649,-20.7650563467883,10.7563532611225));
#176168=CARTESIAN_POINT('Ctrl Pts',(17.5223271831559,-20.6910222879548,
10.7651576708815));
#176169=CARTESIAN_POINT('Ctrl Pts',(17.4389755575171,-20.6298727551388,
10.7718885583543));
#176170=CARTESIAN_POINT('Ctrl Pts',(17.2487296242411,-20.4676541413711,
10.7883751432879));
#176171=CARTESIAN_POINT('Ctrl Pts',(17.1472350425231,-20.3610489322348,
10.7981784475442));
#176172=CARTESIAN_POINT('Ctrl Pts',(17.0481865570513,-20.232608755723,10.8082923099319));
#176173=CARTESIAN_POINT('Ctrl Pts',(17.0389231444625,-20.2203218183561,
10.8092440311345));
#176174=CARTESIAN_POINT('Ctrl Pts',(17.0263864314903,-20.2033104714594,
10.8105389288538));
#176175=CARTESIAN_POINT('Ctrl Pts',(17.0229974326688,-20.1986724556584,
10.8108896812994));
#176176=CARTESIAN_POINT('Ctrl Pts',(17.0176313651076,-20.1912656224869,
10.8114461123316));
#176177=CARTESIAN_POINT('Ctrl Pts',(17.0156420493707,-20.1885057734634,
10.8116526273709));
#176178=CARTESIAN_POINT('Ctrl Pts',(17.0115381591573,-20.1827832690152,
10.8120791264237));
#176179=CARTESIAN_POINT('Ctrl Pts',(17.0094245702003,-20.1798199524105,
10.8122990375342));
#176180=CARTESIAN_POINT('Ctrl Pts',(17.0043917280901,-20.1727251192859,
10.8128233322706));
#176181=CARTESIAN_POINT('Ctrl Pts',(17.0014795978504,-20.1685885288209,
10.8131272277598));
#176182=CARTESIAN_POINT('Ctrl Pts',(16.9916401219008,-20.1545048794572,
10.8141559659486));
#176183=CARTESIAN_POINT('Ctrl Pts',(16.98478324214,-20.1445085657595,10.8148761624763));
#176184=CARTESIAN_POINT('Ctrl Pts',(16.9468326402009,-20.0881505125467,
10.8188842381444));
#176185=CARTESIAN_POINT('Ctrl Pts',(16.9174936642302,-20.0406280304542,
10.8220673839729));
#176186=CARTESIAN_POINT('Ctrl Pts',(16.8017811735682,-19.8354676295683,
10.8352404974851));
#176187=CARTESIAN_POINT('Ctrl Pts',(16.7337847484734,-19.6683315026262,
10.8446698548588));
#176188=CARTESIAN_POINT('Ctrl Pts',(16.6773854537441,-19.4556376310195,
10.8569814738632));
#176189=CARTESIAN_POINT('Ctrl Pts',(16.6681681805087,-19.416384416081,10.8592625142186));
#176190=CARTESIAN_POINT('Ctrl Pts',(16.6588573271048,-19.3709377599084,
10.8619252916509));
#176191=CARTESIAN_POINT('Ctrl Pts',(16.6576628200196,-19.3649768438394,
10.8622749730256));
#176192=CARTESIAN_POINT('Ctrl Pts',(16.6558534175158,-19.3557411096778,
10.8628174635971));
#176193=CARTESIAN_POINT('Ctrl Pts',(16.6552205440034,-19.3524698179488,
10.8630097492605));
#176194=CARTESIAN_POINT('Ctrl Pts',(16.6491723847003,-19.3208065162759,
10.8648722679232));
#176195=CARTESIAN_POINT('Ctrl Pts',(16.6443315774318,-19.2923089722863,
10.8665591904008));
#176196=CARTESIAN_POINT('Ctrl Pts',(16.6385322991908,-19.2533536220153,
10.8688831245356));
#176197=CARTESIAN_POINT('Ctrl Pts',(16.6370657829552,-19.2429738373706,
10.8695040656248));
#176198=CARTESIAN_POINT('Ctrl Pts',(16.6348620662406,-19.2264935135277,
10.8704928377682));
#176199=CARTESIAN_POINT('Ctrl Pts',(16.6340742197072,-19.2203998322545,
10.8708590649165));
#176200=CARTESIAN_POINT('Ctrl Pts',(16.6325483600413,-19.2081797835257,
10.8715947687167));
#176201=CARTESIAN_POINT('Ctrl Pts',(16.6318105821695,-19.2020534480552,
10.871964248942));
#176202=CARTESIAN_POINT('Ctrl Pts',(16.6303836082939,-19.1897513226952,
10.8727075213834));
#176203=CARTESIAN_POINT('Ctrl Pts',(16.6296947992169,-19.1835755504594,
10.8730813219168));
#176204=CARTESIAN_POINT('Ctrl Pts',(16.6281826817397,-19.1694539840531,
10.873937625165));
#176205=CARTESIAN_POINT('Ctrl Pts',(16.627377140809,-19.1615064186572,10.8744206830002));
#176206=CARTESIAN_POINT('Ctrl Pts',(16.6254321893507,-19.1411706930838,
10.8756596692955));
#176207=CARTESIAN_POINT('Ctrl Pts',(16.6243569721826,-19.1287768311628,
10.8764176001408));
#176208=CARTESIAN_POINT('Ctrl Pts',(16.6190952486464,-19.0612149750404,
10.880565036809));
#176209=CARTESIAN_POINT('Ctrl Pts',(16.6169637967638,-19.0059135563383,
10.8840179255723));
#176210=CARTESIAN_POINT('Ctrl Pts',(16.6170004651128,-18.9505966870723,
10.8875305606756));
#176211=CARTESIAN_POINT('Ctrl Pts',(16.7454193692319,-18.2258897639242,
10.9336112441224));
#176212=CARTESIAN_POINT('Ctrl Pts',(16.7173390189837,-18.3027927434369,
10.9286590665973));
#176213=CARTESIAN_POINT('Ctrl Pts',(16.6936915557445,-18.3814141688881,
10.9237068890722));
#176214=CARTESIAN_POINT('Ctrl Pts',(16.6746638753179,-18.4612620601793,
10.9187547115471));
#176215=CARTESIAN_POINT('Ctrl Pts',(16.6556455653778,-18.5410706290957,
10.9138049728012));
#176216=CARTESIAN_POINT('Ctrl Pts',(16.6412426589815,-18.6221042452712,
10.9088552340553));
#176217=CARTESIAN_POINT('Ctrl Pts',(16.631594073455,-18.7038502064707,10.9039054953094));
#176218=CARTESIAN_POINT('Ctrl Pts',(16.6219454879286,-18.7855961676703,
10.8989557565636));
#176219=CARTESIAN_POINT('Ctrl Pts',(16.6170514009679,-18.8680542455025,
10.8940060178177));
#176220=CARTESIAN_POINT('Ctrl Pts',(16.6170004031077,-18.9506935705328,
10.8890562790718));
#176221=CARTESIAN_POINT('Origin',(18.734,-18.952,0.));
#176222=CARTESIAN_POINT('',(16.7454193692303,-18.2258897639288,11.9535387439396));
#176223=CARTESIAN_POINT('',(16.7460270540484,-18.2261211809512,11.7337477306398));
#176224=CARTESIAN_POINT('',(16.7454193692319,-18.2258897639242,0.));
#176225=CARTESIAN_POINT('Ctrl Pts',(16.7454193692303,-18.2258897639288,
11.9535387439396));
#176226=CARTESIAN_POINT('Ctrl Pts',(16.7451290313697,-18.2266849052409,
11.9534866460791));
#176227=CARTESIAN_POINT('Ctrl Pts',(16.7448391690267,-18.2274802245064,
11.9534345739916));
#176228=CARTESIAN_POINT('Ctrl Pts',(16.7420974951151,-18.2350168291508,
11.952941484476));
#176229=CARTESIAN_POINT('Ctrl Pts',(16.7396794456739,-18.2417704693304,
11.9525023189287));
#176230=CARTESIAN_POINT('Ctrl Pts',(16.7359349681624,-18.2523987577304,
11.9518155754438));
#176231=CARTESIAN_POINT('Ctrl Pts',(16.7345854012106,-18.2562651133931,
11.9515666584617));
#176232=CARTESIAN_POINT('Ctrl Pts',(16.7320789914993,-18.2635132174528,
11.9511017521223));
#176233=CARTESIAN_POINT('Ctrl Pts',(16.7309195068626,-18.2668939408757,
11.9508856127554));
#176234=CARTESIAN_POINT('Ctrl Pts',(16.728286071218,-18.2746361171363,11.9503922299608));
#176235=CARTESIAN_POINT('Ctrl Pts',(16.7268177843428,-18.2789994442898,
11.9501153232214));
#176236=CARTESIAN_POINT('Ctrl Pts',(16.7223273436014,-18.2924891612093,
11.9492626928028));
#176237=CARTESIAN_POINT('Ctrl Pts',(16.7193530651715,-18.3016315207151,
11.9486897185535));
#176238=CARTESIAN_POINT('Ctrl Pts',(16.69054739244,-18.3922687618546,11.9430544785594));
#176239=CARTESIAN_POINT('Ctrl Pts',(16.6696094557974,-18.4752476026412,
11.9382547544529));
#176240=CARTESIAN_POINT('Ctrl Pts',(16.6294008149711,-18.6882314405354,
11.9263203751348));
#176241=CARTESIAN_POINT('Ctrl Pts',(16.6170990834496,-18.8191723022085,
11.9193213252498));
#176242=CARTESIAN_POINT('Ctrl Pts',(16.6169313784565,-19.0426470627529,
11.9069620326645));
#176243=CARTESIAN_POINT('Ctrl Pts',(16.6228899848523,-19.1347783275372,
11.9017508294066));
#176244=CARTESIAN_POINT('Ctrl Pts',(16.6366195089841,-19.2398780656785,
11.8955371718309));
#176245=CARTESIAN_POINT('Ctrl Pts',(16.6385368145142,-19.2535173787598,
11.894725675094));
#176246=CARTESIAN_POINT('Ctrl Pts',(16.6418231765904,-19.2753482581545,
11.8934181960775));
#176247=CARTESIAN_POINT('Ctrl Pts',(16.6431076013751,-19.2835523048294,
11.8929248907268));
#176248=CARTESIAN_POINT('Ctrl Pts',(16.6454726643814,-19.2980981837816,
11.8920466993155));
#176249=CARTESIAN_POINT('Ctrl Pts',(16.6465340101666,-19.3044430795483,
11.8916624300161));
#176250=CARTESIAN_POINT('Ctrl Pts',(16.6488043607967,-19.3176455018698,
11.8908602965971));
#176251=CARTESIAN_POINT('Ctrl Pts',(16.6500183113524,-19.3245020890798,
11.8904422793072));
#176252=CARTESIAN_POINT('Ctrl Pts',(16.6532558830817,-19.3422771150747,
11.8893548269423));
#176253=CARTESIAN_POINT('Ctrl Pts',(16.6553316035485,-19.3531857386245,
11.8886837390985));
#176254=CARTESIAN_POINT('Ctrl Pts',(16.6646897658045,-19.4003426339501,
11.8857662647677));
#176255=CARTESIAN_POINT('Ctrl Pts',(16.6728349226117,-19.4364112056578,
11.8834925041284));
#176256=CARTESIAN_POINT('Ctrl Pts',(16.6969459239199,-19.5315155895575,
11.8773804579494));
#176257=CARTESIAN_POINT('Ctrl Pts',(16.7145314150298,-19.590101218353,11.8734934815245));
#176258=CARTESIAN_POINT('Ctrl Pts',(16.786380727417,-19.7965476692969,11.859377500952));
#176259=CARTESIAN_POINT('Ctrl Pts',(16.8545582245221,-19.9390026063447,
11.8488054461995));
#176260=CARTESIAN_POINT('Ctrl Pts',(16.9705616337224,-20.1249378200564,
11.8345700401006));
#176261=CARTESIAN_POINT('Ctrl Pts',(17.0055074777054,-20.1758517555411,
11.8306273573295));
#176262=CARTESIAN_POINT('Ctrl Pts',(17.0481242954733,-20.232466914524,11.8262535703029));
#176263=CARTESIAN_POINT('Ctrl Pts',(17.0536641383772,-20.2397281581677,
11.8256928242317));
#176264=CARTESIAN_POINT('Ctrl Pts',(17.0620088029932,-20.2505202211737,
11.824860027726));
#176265=CARTESIAN_POINT('Ctrl Pts',(17.0647781105656,-20.2540781898058,
11.8245855691298));
#176266=CARTESIAN_POINT('Ctrl Pts',(17.0697578757739,-20.2604341275253,
11.8240955005831));
#176267=CARTESIAN_POINT('Ctrl Pts',(17.0719640466883,-20.2632353734647,
11.8238795937321));
#176268=CARTESIAN_POINT('Ctrl Pts',(17.0767598347342,-20.2692931887643,
11.823412866063));
#176269=CARTESIAN_POINT('Ctrl Pts',(17.079351969474,-20.2725476917915,11.8231622293202));
#176270=CARTESIAN_POINT('Ctrl Pts',(17.0866261911816,-20.2816256494522,
11.8224633512611));
#176271=CARTESIAN_POINT('Ctrl Pts',(17.0913295933534,-20.2874320546423,
11.822016611016));
#176272=CARTESIAN_POINT('Ctrl Pts',(17.1189522583881,-20.3211658070405,
11.8194219537641));
#176273=CARTESIAN_POINT('Ctrl Pts',(17.1425541404909,-20.3485294993241,
11.8173204180937));
#176274=CARTESIAN_POINT('Ctrl Pts',(17.2209741446432,-20.4348768187709,
11.8106490545618));
#176275=CARTESIAN_POINT('Ctrl Pts',(17.2784621466692,-20.4913448228593,
11.8062219730963));
#176276=CARTESIAN_POINT('Ctrl Pts',(17.4407087500992,-20.6334751469453,
11.794464896498));
#176277=CARTESIAN_POINT('Ctrl Pts',(17.5506774578682,-20.7125984704076,
11.7872133859732));
#176278=CARTESIAN_POINT('Ctrl Pts',(17.7219081254075,-20.8124664558866,
11.7760629870063));
#176279=CARTESIAN_POINT('Ctrl Pts',(17.777766999318,-20.8417837811185,11.7724493392766));
#176280=CARTESIAN_POINT('Ctrl Pts',(17.8461536649455,-20.8738672831149,
11.7680131790284));
#176281=CARTESIAN_POINT('Ctrl Pts',(17.8575065016266,-20.879071380587,11.7672764012017));
#176282=CARTESIAN_POINT('Ctrl Pts',(17.8762116380342,-20.8874462594529,
11.7660616347395));
#176283=CARTESIAN_POINT('Ctrl Pts',(17.8835371573524,-20.8906763648784,
11.7655856854802));
#176284=CARTESIAN_POINT('Ctrl Pts',(17.8967322236305,-20.896405401417,11.7647279354952));
#176285=CARTESIAN_POINT('Ctrl Pts',(17.9025951038541,-20.8989195134094,
11.7643466590406));
#176286=CARTESIAN_POINT('Ctrl Pts',(17.9150971796616,-20.9042138660923,
11.7635332452201));
#176287=CARTESIAN_POINT('Ctrl Pts',(17.9217393573994,-20.9069868169915,
11.7631008656941));
#176288=CARTESIAN_POINT('Ctrl Pts',(17.9396435922347,-20.9143544127663,
11.7619347039349));
#176289=CARTESIAN_POINT('Ctrl Pts',(17.9509311927632,-20.9188859085661,
11.7611987975757));
#176290=CARTESIAN_POINT('Ctrl Pts',(18.007271272777,-20.9409422284897,11.7575216573875));
#176291=CARTESIAN_POINT('Ctrl Pts',(18.0528727102851,-20.9570164206582,
11.7545322772497));
#176292=CARTESIAN_POINT('Ctrl Pts',(18.185439492042,-20.9987008622925,11.7457982265456));
#176293=CARTESIAN_POINT('Ctrl Pts',(18.2735448375389,-21.0203038846941,
11.7399361868778));
#176294=CARTESIAN_POINT('Ctrl Pts',(18.5213236825052,-21.0644392688341,
11.7234139481658));
#176295=CARTESIAN_POINT('Ctrl Pts',(18.6826011555627,-21.0744968926795,
11.7125878646361));
#176296=CARTESIAN_POINT('Ctrl Pts',(18.8634464080747,-21.0651334635202,
11.7012277896952));
#176297=CARTESIAN_POINT('Ctrl Pts',(18.8834149961614,-21.0638154827722,
11.6999848545792));
#176298=CARTESIAN_POINT('Ctrl Pts',(18.9097245880237,-21.0617039136759,
11.698364925974));
#176299=CARTESIAN_POINT('Ctrl Pts',(18.9160842203008,-21.0611645439232,
11.6979747189619));
#176300=CARTESIAN_POINT('Ctrl Pts',(18.9263451340498,-21.0602475448066,
11.6973474550377));
#176301=CARTESIAN_POINT('Ctrl Pts',(18.9302479191835,-21.0598878327771,
11.6971094130369));
#176302=CARTESIAN_POINT('Ctrl Pts',(18.9377538248305,-21.0591750011801,
11.6966526763518));
#176303=CARTESIAN_POINT('Ctrl Pts',(18.9413570417738,-21.0588234772036,
11.6964338976899));
#176304=CARTESIAN_POINT('Ctrl Pts',(18.9498791280524,-21.0579700019049,
11.6959175580283));
#176305=CARTESIAN_POINT('Ctrl Pts',(18.9547972090244,-21.0574600543514,
11.6956204459109));
#176306=CARTESIAN_POINT('Ctrl Pts',(18.971104141749,-21.0557114498484,11.6946380503377));
#176307=CARTESIAN_POINT('Ctrl Pts',(18.9824849514607,-21.0543975552393,
11.6939568638423));
#176308=CARTESIAN_POINT('Ctrl Pts',(19.1213023619589,-21.0372283395965,
11.6856962451954));
#176309=CARTESIAN_POINT('Ctrl Pts',(19.2470709261268,-21.0098989680273,
11.6786989162827));
#176310=CARTESIAN_POINT('Ctrl Pts',(19.5269345964225,-20.9218096773956,
11.6627560944265));
#176311=CARTESIAN_POINT('Ctrl Pts',(19.67792252022,-20.8540774792264,11.6538404551469));
#176312=CARTESIAN_POINT('Ctrl Pts',(19.8397851365438,-20.7574045920512,
11.6428917697373));
#176313=CARTESIAN_POINT('Ctrl Pts',(19.8598518696124,-20.7449595675927,
11.6415090402226));
#176314=CARTESIAN_POINT('Ctrl Pts',(19.8878195113245,-20.7269598977285,
11.639543872987));
#176315=CARTESIAN_POINT('Ctrl Pts',(19.8958974415166,-20.7216825800045,
11.6389717198014));
#176316=CARTESIAN_POINT('Ctrl Pts',(19.9089274486118,-20.7130423953321,
11.6380412851637));
#176317=CARTESIAN_POINT('Ctrl Pts',(19.913901893711,-20.7097133861192,11.6376842783305));
#176318=CARTESIAN_POINT('Ctrl Pts',(19.9242561526218,-20.7027203255881,
11.6369373781025));
#176319=CARTESIAN_POINT('Ctrl Pts',(19.9296333128062,-20.6990524740605,
11.6365473433291));
#176320=CARTESIAN_POINT('Ctrl Pts',(19.9423332736559,-20.6903035236184,
11.635620978014));
#176321=CARTESIAN_POINT('Ctrl Pts',(19.9496410260951,-20.6852008920854,
11.6350838300585));
#176322=CARTESIAN_POINT('Ctrl Pts',(19.9739137702612,-20.6680234415619,
11.633285799285));
#176323=CARTESIAN_POINT('Ctrl Pts',(19.9907323859878,-20.6557447787339,
11.6320170992865));
#176324=CARTESIAN_POINT('Ctrl Pts',(20.0798208976864,-20.5886675688534,
11.6251710596367));
#176325=CARTESIAN_POINT('Ctrl Pts',(20.1486853110398,-20.5295222361244,
11.6194228779019));
#176326=CARTESIAN_POINT('Ctrl Pts',(20.311924953861,-20.3700140739128,11.6046262247822));
#176327=CARTESIAN_POINT('Ctrl Pts',(20.4007047734906,-20.2645176635251,
11.595426390967));
#176328=CARTESIAN_POINT('Ctrl Pts',(20.4911335336766,-20.1329568415172,
11.5850001177481));
#176329=CARTESIAN_POINT('Ctrl Pts',(20.5033652197423,-20.1145506799144,
11.5835638053869));
#176330=CARTESIAN_POINT('Ctrl Pts',(20.5431736663893,-20.0525631052629,
11.5788081830348));
#176331=CARTESIAN_POINT('Ctrl Pts',(20.5694482699565,-20.0081624399646,
11.5755333908071));
#176332=CARTESIAN_POINT('Ctrl Pts',(20.5982039387647,-19.9552484138165,
11.5718189370328));
#176333=CARTESIAN_POINT('Ctrl Pts',(20.6022845056128,-19.9476288048573,
11.5712885005483));
#176334=CARTESIAN_POINT('Ctrl Pts',(20.6084028878481,-19.9360339244516,
11.5704882925831));
#176335=CARTESIAN_POINT('Ctrl Pts',(20.6104749198411,-19.9320769492741,
11.5702164286705));
#176336=CARTESIAN_POINT('Ctrl Pts',(20.6141772140292,-19.9249518682232,
11.5697291347125));
#176337=CARTESIAN_POINT('Ctrl Pts',(20.6158120076387,-19.9217861942259,
11.5695134222468));
#176338=CARTESIAN_POINT('Ctrl Pts',(20.6193531971344,-19.9148862344291,
11.569044977352));
#176339=CARTESIAN_POINT('Ctrl Pts',(20.6212564878531,-19.9111504199832,
11.5687924405615));
#176340=CARTESIAN_POINT('Ctrl Pts',(20.6265875001978,-19.9006093055345,
11.5680828740836));
#176341=CARTESIAN_POINT('Ctrl Pts',(20.6299896370554,-19.8937910387281,
11.5676274205919));
#176342=CARTESIAN_POINT('Ctrl Pts',(20.6504355311775,-19.8522553139292,
11.5648732652217));
#176343=CARTESIAN_POINT('Ctrl Pts',(20.6665632688079,-19.8170921409814,
11.5626278582963));
#176344=CARTESIAN_POINT('Ctrl Pts',(20.7171525708346,-19.6983058236882,
11.5552628194603));
#176345=CARTESIAN_POINT('Ctrl Pts',(20.7472212624142,-19.6129154630708,
11.5503221825712));
#176346=CARTESIAN_POINT('Ctrl Pts',(20.8179978025325,-19.3615918143733,
11.5361254691591));
#176347=CARTESIAN_POINT('Ctrl Pts',(20.8442214334236,-19.1923558174504,
11.5269280730812));
#176348=CARTESIAN_POINT('Ctrl Pts',(20.8506174542962,-18.9985100483466,
11.5156614898658));
#176349=CARTESIAN_POINT('Ctrl Pts',(20.8510012979536,-18.9751964095409,
11.5142958082286));
#176350=CARTESIAN_POINT('Ctrl Pts',(20.8509994609138,-18.9422820921322,
11.5123508577701));
#176351=CARTESIAN_POINT('Ctrl Pts',(20.8509336285808,-18.9326825774612,
11.5117815872653));
#176352=CARTESIAN_POINT('Ctrl Pts',(20.8507208748756,-18.9171079139512,
11.5108545758878));
#176353=CARTESIAN_POINT('Ctrl Pts',(20.8506139347375,-18.9111322871954,
11.5104980910136));
#176354=CARTESIAN_POINT('Ctrl Pts',(20.8503375057484,-18.8986424830744,
11.5097512605741));
#176355=CARTESIAN_POINT('Ctrl Pts',(20.8501632410867,-18.8921284838209,
11.5093607691106));
#176356=CARTESIAN_POINT('Ctrl Pts',(20.84967812505,-18.876665765734,11.5084314482702));
#176357=CARTESIAN_POINT('Ctrl Pts',(20.8493405699849,-18.8677180636594,
11.507891787315));
#176358=CARTESIAN_POINT('Ctrl Pts',(20.8480186877883,-18.8377299039485,
11.5060766111868));
#176359=CARTESIAN_POINT('Ctrl Pts',(20.8467771350606,-18.8167025705487,
11.5047930734651));
#176360=CARTESIAN_POINT('Ctrl Pts',(20.8383803990078,-18.703285233948,11.4978096228056));
#176361=CARTESIAN_POINT('Ctrl Pts',(20.8254795101571,-18.6114336461119,
11.4919310928861));
#176362=CARTESIAN_POINT('Ctrl Pts',(20.775836577602,-18.3728574942928,11.4761164732412));
#176363=CARTESIAN_POINT('Ctrl Pts',(20.7293326848203,-18.2287114025861,
11.4659781783952));
#176364=CARTESIAN_POINT('Ctrl Pts',(20.6444862812803,-18.0381945165704,
11.4524640226368));
#176365=CARTESIAN_POINT('Ctrl Pts',(20.618948293174,-17.9866143313949,11.4487979893458));
#176366=CARTESIAN_POINT('Ctrl Pts',(20.587077525497,-17.9283440397123,11.4446996785264));
#176367=CARTESIAN_POINT('Ctrl Pts',(20.5827676794663,-17.9205806312505,
11.4441545793538));
#176368=CARTESIAN_POINT('Ctrl Pts',(20.5761916553775,-17.9089087715374,
11.4433367157967));
#176369=CARTESIAN_POINT('Ctrl Pts',(20.5739616657005,-17.9049801932793,
11.4430617211631));
#176370=CARTESIAN_POINT('Ctrl Pts',(20.569948658204,-17.8979628833771,11.4425710751942));
#176371=CARTESIAN_POINT('Ctrl Pts',(20.5681704008008,-17.8948715025046,
11.442355123973));
#176372=CARTESIAN_POINT('Ctrl Pts',(20.5643038219199,-17.8881888433521,
11.4418887318417));
#176373=CARTESIAN_POINT('Ctrl Pts',(20.5622127458144,-17.8845992250958,
11.4416384726911));
#176374=CARTESIAN_POINT('Ctrl Pts',(20.5563457178263,-17.874595487962,11.4409417127407));
#176375=CARTESIAN_POINT('Ctrl Pts',(20.5525464433895,-17.8681950199373,
11.4404966983238));
#176376=CARTESIAN_POINT('Ctrl Pts',(20.5303560265555,-17.8312570386012,
11.4379321829172));
#176377=CARTESIAN_POINT('Ctrl Pts',(20.5112284850662,-17.8011659502717,
11.4358578136591));
#176378=CARTESIAN_POINT('Ctrl Pts',(20.4474450096976,-17.7062091528249,
11.429311978285));
#176379=CARTESIAN_POINT('Ctrl Pts',(20.3999252865499,-17.6433428612584,
11.4249771496786));
#176380=CARTESIAN_POINT('Ctrl Pts',(20.2276281177025,-17.4400442664173,
11.4104428664405));
#176381=CARTESIAN_POINT('Ctrl Pts',(20.0877502995649,-17.3136198827431,
11.4004124995281));
#176382=CARTESIAN_POINT('Ctrl Pts',(19.9150047501476,-17.1949013545242,
11.388218921189));
#176383=CARTESIAN_POINT('Ctrl Pts',(19.8967794471314,-17.1827878096589,
11.3869359264506));
#176384=CARTESIAN_POINT('Ctrl Pts',(19.8712833607534,-17.1664058374112,
11.3851443884386));
#176385=CARTESIAN_POINT('Ctrl Pts',(19.8641695629118,-17.1618947762579,
11.3846448734637));
#176386=CARTESIAN_POINT('Ctrl Pts',(19.8518846932427,-17.1542070080992,
11.3837827731188));
#176387=CARTESIAN_POINT('Ctrl Pts',(19.8467264999286,-17.151009837814,11.3834209479963));
#176388=CARTESIAN_POINT('Ctrl Pts',(19.8360543094168,-17.1444583118117,
11.382672623711));
#176389=CARTESIAN_POINT('Ctrl Pts',(19.8305385824702,-17.1411069078584,
11.3822860212385));
#176390=CARTESIAN_POINT('Ctrl Pts',(19.8176502736626,-17.1333563318903,
11.3813829850102));
#176391=CARTESIAN_POINT('Ctrl Pts',(19.8102661239642,-17.1289767049816,
11.3808658450498));
#176392=CARTESIAN_POINT('Ctrl Pts',(19.7864755946789,-17.1150611814342,
11.3792003487391));
#176393=CARTESIAN_POINT('Ctrl Pts',(19.7699679215923,-17.1057011268004,
11.378045668821));
#176394=CARTESIAN_POINT('Ctrl Pts',(19.6864705672357,-17.0598294448661,
11.3722084542298));
#176395=CARTESIAN_POINT('Ctrl Pts',(19.6176745788376,-17.0267398669967,
11.3674064393238));
#176396=CARTESIAN_POINT('Ctrl Pts',(19.4458934726787,-16.9552656247558,
11.3554427339591));
#176397=CARTESIAN_POINT('Ctrl Pts',(19.3414175873303,-16.9210443378806,
11.3481824164327));
#176398=CARTESIAN_POINT('Ctrl Pts',(19.1693169898725,-16.8791454418259,
11.3364828919027));
#176399=CARTESIAN_POINT('Ctrl Pts',(19.1031384871142,-16.866343149384,11.3320467893725));
#176400=CARTESIAN_POINT('Ctrl Pts',(19.035577865389,-16.8565905925698,11.3276415407469));
#176401=CARTESIAN_POINT('Ctrl Pts',(19.0346960587832,-16.8564638695848,
11.3275840644883));
#176402=CARTESIAN_POINT('Ctrl Pts',(19.0183690273553,-16.8541280565072,
11.3265202656629));
#176403=CARTESIAN_POINT('Ctrl Pts',(19.002899569418,-16.8520891736199,11.3255189494647));
#176404=CARTESIAN_POINT('Ctrl Pts',(18.9515895239313,-16.8459027897029,
11.3222224409731));
#176405=CARTESIAN_POINT('Ctrl Pts',(18.9156633223501,-16.8425001885016,
11.3199540831028));
#176406=CARTESIAN_POINT('Ctrl Pts',(18.8725846449321,-16.839529012918,11.3172952456587));
#176407=CARTESIAN_POINT('Ctrl Pts',(18.8655014001075,-16.8390762531264,
11.3168600390575));
#176408=CARTESIAN_POINT('Ctrl Pts',(18.8539248818732,-16.8383947242109,
11.3161521310599));
#176409=CARTESIAN_POINT('Ctrl Pts',(18.8494329856097,-16.8381446440607,
11.3158782792194));
#176410=CARTESIAN_POINT('Ctrl Pts',(18.8413802010849,-16.837722061443,11.315388862573));
#176411=CARTESIAN_POINT('Ctrl Pts',(18.8378196576743,-16.8375442335365,
11.3151730042479));
#176412=CARTESIAN_POINT('Ctrl Pts',(18.8300953662342,-16.8371780093704,
11.3147058890192));
#176413=CARTESIAN_POINT('Ctrl Pts',(18.8259315192207,-16.8369929153963,
11.3144548188415));
#176414=CARTESIAN_POINT('Ctrl Pts',(18.8142677900671,-16.8365089415146,
11.3137535070402));
#176415=CARTESIAN_POINT('Ctrl Pts',(18.8067667393094,-16.8362376451665,
11.3133047834457));
#176416=CARTESIAN_POINT('Ctrl Pts',(18.7625926037332,-16.8348751680644,
11.3106749145689));
#176417=CARTESIAN_POINT('Ctrl Pts',(18.7258951899899,-16.8346975251789,
11.308541633289));
#176418=CARTESIAN_POINT('Ctrl Pts',(18.6066075792878,-16.837221933677,11.3017214832842));
#176419=CARTESIAN_POINT('Ctrl Pts',(18.5241722098006,-16.8438041974536,
11.2971847810895));
#176420=CARTESIAN_POINT('Ctrl Pts',(18.262198199831,-16.8802455989509,11.2827770310715));
#176421=CARTESIAN_POINT('Ctrl Pts',(18.0860701303168,-16.9284032516508,
11.2730315254473));
#176422=CARTESIAN_POINT('Ctrl Pts',(17.8975352559485,-17.007129710186,11.2611530364774));
#176423=CARTESIAN_POINT('Ctrl Pts',(17.8769439725337,-17.0161155455159,
11.259836402694));
#176424=CARTESIAN_POINT('Ctrl Pts',(17.8478917470067,-17.0293480184882,
11.2579495247959));
#176425=CARTESIAN_POINT('Ctrl Pts',(17.8393098243508,-17.0333265094823,
11.2573884766855));
#176426=CARTESIAN_POINT('Ctrl Pts',(17.8253726254387,-17.0399014902429,
11.2564712095513));
#176427=CARTESIAN_POINT('Ctrl Pts',(17.8200010668774,-17.0424633111787,
11.2561161939027));
#176428=CARTESIAN_POINT('Ctrl Pts',(17.8088683755985,-17.0478304860607,
11.2553772810711));
#176429=CARTESIAN_POINT('Ctrl Pts',(17.8031090417456,-17.0506394127566,
11.2549932622602));
#176430=CARTESIAN_POINT('Ctrl Pts',(17.7894934637189,-17.057356656793,11.2540812020395));
#176431=CARTESIAN_POINT('Ctrl Pts',(17.781648636919,-17.0612877340402,11.2535523681956));
#176432=CARTESIAN_POINT('Ctrl Pts',(17.7650495022696,-17.069735150008,11.2524262017514));
#176433=CARTESIAN_POINT('Ctrl Pts',(17.7563018463904,-17.074264036706,11.2518284358722));
#176434=CARTESIAN_POINT('Ctrl Pts',(17.7325789402395,-17.08675670847,11.2501955197829));
#176435=CARTESIAN_POINT('Ctrl Pts',(17.7176675222309,-17.0948395481439,
11.2491561902378));
#176436=CARTESIAN_POINT('Ctrl Pts',(17.6711091087536,-17.1208055174505,
11.2458696200076));
#176437=CARTESIAN_POINT('Ctrl Pts',(17.6398259276486,-17.1393243175908,
11.2436002440543));
#176438=CARTESIAN_POINT('Ctrl Pts',(17.5216997100359,-17.2134240963125,
11.234792448448));
#176439=CARTESIAN_POINT('Ctrl Pts',(17.4384910833157,-17.2745106271483,
11.2280708160822));
#176440=CARTESIAN_POINT('Ctrl Pts',(17.2484788401491,-17.4366021491222,
11.2116009775031));
#176441=CARTESIAN_POINT('Ctrl Pts',(17.1470748224785,-17.5431427985949,
11.2018054480092));
#176442=CARTESIAN_POINT('Ctrl Pts',(17.0481227365419,-17.6714756891822,
11.1917010530353));
#176443=CARTESIAN_POINT('Ctrl Pts',(17.0388812168322,-17.6837346491298,
11.1907515613367));
#176444=CARTESIAN_POINT('Ctrl Pts',(17.0263690634383,-17.7007132551913,
11.1894591898376));
#176445=CARTESIAN_POINT('Ctrl Pts',(17.0229833141161,-17.7053469465696,
11.1891087715995));
#176446=CARTESIAN_POINT('Ctrl Pts',(17.0176211044971,-17.7127485913637,
11.188552738323));
#176447=CARTESIAN_POINT('Ctrl Pts',(17.0156324285234,-17.7155075995335,
11.1883462889346));
#176448=CARTESIAN_POINT('Ctrl Pts',(17.0115287800884,-17.7212298548417,
11.1879198135975));
#176449=CARTESIAN_POINT('Ctrl Pts',(17.0094148001329,-17.7241937684648,
11.1876998610218));
#176450=CARTESIAN_POINT('Ctrl Pts',(17.0043792803727,-17.7312925010446,
11.1871752852511));
#176451=CARTESIAN_POINT('Ctrl Pts',(17.001464883944,-17.7354324085303,11.1868711515815));
#176452=CARTESIAN_POINT('Ctrl Pts',(16.9916096540791,-17.7495390273418,
11.1858407586687));
#176453=CARTESIAN_POINT('Ctrl Pts',(16.9847395997665,-17.7595552104824,
11.1851191658798));
#176454=CARTESIAN_POINT('Ctrl Pts',(16.9466622529028,-17.8161073145345,
11.1810975798336));
#176455=CARTESIAN_POINT('Ctrl Pts',(16.9172232111286,-17.8638126894764,
11.1779030951105));
#176456=CARTESIAN_POINT('Ctrl Pts',(16.8331218727429,-18.013045296126,11.1683245428783));
#176457=CARTESIAN_POINT('Ctrl Pts',(16.7848807143242,-18.1178179015326,
11.1621510647684));
#176458=CARTESIAN_POINT('Ctrl Pts',(16.7454193125899,-18.2258899190484,
11.1558808694255));
#176459=CARTESIAN_POINT('',(16.6169841393337,-18.9509245720249,11.6890562438269));
#176460=CARTESIAN_POINT('Ctrl Pts',(16.6170002731508,-18.9509245835716,
11.6890562436247));
#176461=CARTESIAN_POINT('Ctrl Pts',(16.6169638390757,-19.0226464998436,
11.6847206650338));
#176462=CARTESIAN_POINT('Ctrl Pts',(16.6205764456708,-19.0945164382378,
11.680385086443));
#176463=CARTESIAN_POINT('Ctrl Pts',(16.6278569147557,-19.1661268420297,
11.6760495078521));
#176464=CARTESIAN_POINT('Ctrl Pts',(16.6351262827891,-19.2376280563218,
11.6717205400277));
#176465=CARTESIAN_POINT('Ctrl Pts',(16.6460523594263,-19.3088700336267,
11.6673915722034));
#176466=CARTESIAN_POINT('Ctrl Pts',(16.6606019569669,-19.3794453826474,
11.663062604379));
#176467=CARTESIAN_POINT('Ctrl Pts',(16.6751392352657,-19.4499609750466,
11.6587373019208));
#176468=CARTESIAN_POINT('Ctrl Pts',(16.6932938534711,-19.5198105757981,
11.6544119994625));
#176469=CARTESIAN_POINT('Ctrl Pts',(16.7149810087477,-19.588593522558,11.6500866970042));
#176470=CARTESIAN_POINT('Ctrl Pts',(16.7366573538933,-19.6573421839236,
11.6457635505266));
#176471=CARTESIAN_POINT('Ctrl Pts',(16.7618625956117,-19.725024774734,11.6414404040489));
#176472=CARTESIAN_POINT('Ctrl Pts',(16.7904616388555,-19.7912542158128,
11.6371172575713));
#176473=CARTESIAN_POINT('Ctrl Pts',(16.8190563851712,-19.8574737060992,
11.6327947606345));
#176474=CARTESIAN_POINT('Ctrl Pts',(16.8510437238668,-19.9222400264108,
11.6284722636978));
#176475=CARTESIAN_POINT('Ctrl Pts',(16.8862405216003,-19.9851862900678,
11.6241497667611));
#176476=CARTESIAN_POINT('Ctrl Pts',(16.9214689659601,-20.0481891508306,
11.6198233833218));
#176477=CARTESIAN_POINT('Ctrl Pts',(16.9599123931247,-20.1093682524578,
11.6154969998825));
#176478=CARTESIAN_POINT('Ctrl Pts',(17.0013422781536,-20.1683824311975,
11.6111706164432));
#176479=CARTESIAN_POINT('Ctrl Pts',(17.0427896393186,-20.2274215035574,
11.6068424080298));
#176480=CARTESIAN_POINT('Ctrl Pts',(17.0872256618383,-20.2842934442302,
11.6025141996165));
#176481=CARTESIAN_POINT('Ctrl Pts',(17.1343808833966,-20.3386894684092,
11.5981859912031));
#176482=CARTESIAN_POINT('Ctrl Pts',(17.1816225942444,-20.3931852625252,
11.5938498442485));
#176483=CARTESIAN_POINT('Ctrl Pts',(17.2315931237805,-20.4451957108515,
11.5895136972939));
#176484=CARTESIAN_POINT('Ctrl Pts',(17.2839858438636,-20.4944486853714,
11.5851775503393));
#176485=CARTESIAN_POINT('Ctrl Pts',(17.3330384860336,-20.5405617432754,
11.5811178362297));
#176486=CARTESIAN_POINT('Ctrl Pts',(17.3842137273589,-20.584257877088,11.5770581221201));
#176487=CARTESIAN_POINT('Ctrl Pts',(17.4372361998843,-20.6253477363386,
11.5729984080105));
#176488=CARTESIAN_POINT('Ctrl Pts',(17.494549025663,-20.6697624124625,11.5686101990796));
#176489=CARTESIAN_POINT('Ctrl Pts',(17.5542581954977,-20.7113158984435,
11.5642219901487));
#176490=CARTESIAN_POINT('Ctrl Pts',(17.6160462231313,-20.7497397900656,
11.5598337812178));
#176491=CARTESIAN_POINT('Ctrl Pts',(17.6777425470871,-20.7881066542617,
11.5554520851166));
#176492=CARTESIAN_POINT('Ctrl Pts',(17.7415111977165,-20.8233528921038,
11.5510703890153));
#176493=CARTESIAN_POINT('Ctrl Pts',(17.8070029012398,-20.8552512653063,
11.546688692914));
#176494=CARTESIAN_POINT('Ctrl Pts',(17.8724176467993,-20.8871121553817,
11.5423121456544));
#176495=CARTESIAN_POINT('Ctrl Pts',(17.9395509916041,-20.9156327855723,
11.5379355983948));
#176496=CARTESIAN_POINT('Ctrl Pts',(18.00802753011,-20.9406309292983,11.5335590511351));
#176497=CARTESIAN_POINT('Ctrl Pts',(18.0764606417904,-20.9656132195649,
11.5291852794182));
#176498=CARTESIAN_POINT('Ctrl Pts',(18.14623480501,-20.9870772907212,11.5248115077012));
#176499=CARTESIAN_POINT('Ctrl Pts',(18.2169543269187,-21.0048888844621,
11.5204377359842));
#176500=CARTESIAN_POINT('Ctrl Pts',(18.2876523286393,-21.0226950580752,
11.5160652952207));
#176501=CARTESIAN_POINT('Ctrl Pts',(18.3592946504355,-21.0368508431231,
11.5116928544571));
#176502=CARTESIAN_POINT('Ctrl Pts',(18.4314717388382,-21.0472722141045,
11.5073204136936));
#176503=CARTESIAN_POINT('Ctrl Pts',(18.5036506728172,-21.0576938515615,
11.5029478611262));
#176504=CARTESIAN_POINT('Ctrl Pts',(18.5763639228387,-21.0643808184122,
11.4985753085589));
#176505=CARTESIAN_POINT('Ctrl Pts',(18.6491947479433,-21.0673007042082,
11.4942027559915));
#176506=CARTESIAN_POINT('Ctrl Pts',(18.7221011596252,-21.0702236203718,
11.4898256654242));
#176507=CARTESIAN_POINT('Ctrl Pts',(18.7951249069974,-21.0693716302984,
11.4854485748569));
#176508=CARTESIAN_POINT('Ctrl Pts',(18.8678480060375,-21.0647644713218,
11.4810714842896));
#176509=CARTESIAN_POINT('Ctrl Pts',(18.9406108218612,-21.0601547962048,
11.4766920032306));
#176510=CARTESIAN_POINT('Ctrl Pts',(19.0130721829174,-21.0517859243704,
11.4723125221717));
#176511=CARTESIAN_POINT('Ctrl Pts',(19.084820705146,-21.0397293485605,11.4679330411128));
#176512=CARTESIAN_POINT('Ctrl Pts',(19.1566964011486,-21.0276514025509,
11.463545797453));
#176513=CARTESIAN_POINT('Ctrl Pts',(19.227856263807,-21.0118728040952,11.4591585537933));
#176514=CARTESIAN_POINT('Ctrl Pts',(19.2979011262233,-20.9925157484921,
11.4547713101336));
#176515=CARTESIAN_POINT('Ctrl Pts',(19.3455248831596,-20.9793548159233,
11.4517884071988));
#176516=CARTESIAN_POINT('Ctrl Pts',(19.3926335158208,-20.9645407241657,
11.4488055042639));
#176517=CARTESIAN_POINT('Ctrl Pts',(19.4391069833085,-20.9481245307068,
11.4458226013291));
#176518=CARTESIAN_POINT('Ctrl Pts',(19.507475042724,-20.9239743359732,11.4414343923982));
#176519=CARTESIAN_POINT('Ctrl Pts',(19.5747343896099,-20.8962604871605,
11.4370461834673));
#176520=CARTESIAN_POINT('Ctrl Pts',(19.6404874892068,-20.8651046578563,
11.4326579745364));
#176521=CARTESIAN_POINT('Ctrl Pts',(19.7061430003018,-20.8339950689686,
11.4282762784352));
#176522=CARTESIAN_POINT('Ctrl Pts',(19.7702962696065,-20.7994538454432,
11.4238945823339));
#176523=CARTESIAN_POINT('Ctrl Pts',(19.8325671704115,-20.761651671481,11.4195128862326));
#176524=CARTESIAN_POINT('Ctrl Pts',(19.8947648979524,-20.7238939180816,
11.415136338973));
#176525=CARTESIAN_POINT('Ctrl Pts',(19.9550842407134,-20.6828830753685,
11.4107597917133));
#176526=CARTESIAN_POINT('Ctrl Pts',(20.013168775078,-20.6388361642037,11.4063832444537));
#176527=CARTESIAN_POINT('Ctrl Pts',(20.071216473075,-20.5948171869499,11.4020094727367));
#176528=CARTESIAN_POINT('Ctrl Pts',(20.1270317913337,-20.5477662523015,
11.3976357010197));
#176529=CARTESIAN_POINT('Ctrl Pts',(20.1802876588313,-20.4979434038516,
11.3932619293028));
#176530=CARTESIAN_POINT('Ctrl Pts',(20.2335273203897,-20.4481357166618,
11.3888894885392));
#176531=CARTESIAN_POINT('Ctrl Pts',(20.2842087253977,-20.395558119635,11.3845170477756));
#176532=CARTESIAN_POINT('Ctrl Pts',(20.3320395381811,-20.3405095010154,
11.3801446070121));
#176533=CARTESIAN_POINT('Ctrl Pts',(20.3798715740035,-20.2854594747966,
11.3757720544447));
#176534=CARTESIAN_POINT('Ctrl Pts',(20.4248525580102,-20.2279386669777,
11.3713995018774));
#176535=CARTESIAN_POINT('Ctrl Pts',(20.4667296641659,-20.1682799475942,
11.3670269493101));
#176536=CARTESIAN_POINT('Ctrl Pts',(20.5086502319619,-20.1085593121413,
11.3626498587427));
#176537=CARTESIAN_POINT('Ctrl Pts',(20.5474602125882,-20.0466967307923,
11.3582727681754));
#176538=CARTESIAN_POINT('Ctrl Pts',(20.5829499551954,-19.9830543454071,
11.3538956776081));
#176539=CARTESIAN_POINT('Ctrl Pts',(20.6184590800683,-19.9193772025531,
11.3495161965491));
#176540=CARTESIAN_POINT('Ctrl Pts',(20.6506441436595,-19.8539187535681,
11.3451367154902));
#176541=CARTESIAN_POINT('Ctrl Pts',(20.6793425856619,-19.7870636050088,
11.3407572344312));
#176542=CARTESIAN_POINT('Ctrl Pts',(20.7080918954601,-19.7200899561474,
11.3363699907715));
#176543=CARTESIAN_POINT('Ctrl Pts',(20.7333420751796,-19.6517151168647,
11.3319827471118));
#176544=CARTESIAN_POINT('Ctrl Pts',(20.7549798102578,-19.58234086535,11.327595503452));
#176545=CARTESIAN_POINT('Ctrl Pts',(20.7696913851038,-19.5351730592071,
11.3246126005172));
#176546=CARTESIAN_POINT('Ctrl Pts',(20.7827340876901,-19.4875435673451,
11.3216296975824));
#176547=CARTESIAN_POINT('Ctrl Pts',(20.7940858734221,-19.4395809616124,
11.3186467946476));
#176548=CARTESIAN_POINT('Ctrl Pts',(20.8107857153611,-19.3690222007593,
11.3142585857167));
#176549=CARTESIAN_POINT('Ctrl Pts',(20.8238889631161,-19.2974667533231,
11.3098703767858));
#176550=CARTESIAN_POINT('Ctrl Pts',(20.8332827468938,-19.2253147427305,
11.3054821678549));
#176551=CARTESIAN_POINT('Ctrl Pts',(20.8426625887389,-19.1532698176848,
11.3011004717537));
#176552=CARTESIAN_POINT('Ctrl Pts',(20.8483438339328,-19.0806305615065,
11.2967187756524));
#176553=CARTESIAN_POINT('Ctrl Pts',(20.8502642454991,-19.0078089887226,
11.2923370795512));
#176554=CARTESIAN_POINT('Ctrl Pts',(20.8521824004289,-18.9350729870818,
11.2879605322915));
#176555=CARTESIAN_POINT('Ctrl Pts',(20.8503484880034,-18.8621555742344,
11.2835839850319));
#176556=CARTESIAN_POINT('Ctrl Pts',(20.84475206308,-18.789473915313,11.2792074377723));
#176557=CARTESIAN_POINT('Ctrl Pts',(20.8391591873278,-18.7168383500433,
11.2748336660553));
#176558=CARTESIAN_POINT('Ctrl Pts',(20.8298085704126,-18.6444387218197,
11.2704598943383));
#176559=CARTESIAN_POINT('Ctrl Pts',(20.816741830502,-18.5726908022771,11.2660861226214));
#176560=CARTESIAN_POINT('Ctrl Pts',(20.8036790668443,-18.5009647158674,
11.2617136818578));
#176561=CARTESIAN_POINT('Ctrl Pts',(20.786902511612,-18.4298904187043,11.2573412410943));
#176562=CARTESIAN_POINT('Ctrl Pts',(20.7665052467622,-18.3598755013645,
11.2529688003307));
#176563=CARTESIAN_POINT('Ctrl Pts',(20.7461074603521,-18.2898587937358,
11.2485962477634));
#176564=CARTESIAN_POINT('Ctrl Pts',(20.7220889173527,-18.2209019822774,
11.244223695196));
#176565=CARTESIAN_POINT('Ctrl Pts',(20.6945926588482,-18.1533978299111,
11.2398511426287));
#176566=CARTESIAN_POINT('Ctrl Pts',(20.6670678636894,-18.0858236191891,
11.2354740520614));
#176567=CARTESIAN_POINT('Ctrl Pts',(20.6360583291642,-18.0197055253275,
11.2310969614941));
#176568=CARTESIAN_POINT('Ctrl Pts',(20.6017550792382,-17.9554158520327,
11.2267198709267));
#176569=CARTESIAN_POINT('Ctrl Pts',(20.5674330950343,-17.8910910677612,
11.2223403898678));
#176570=CARTESIAN_POINT('Ctrl Pts',(20.5298140629461,-17.8285971057597,
11.2179609088089));
#176571=CARTESIAN_POINT('Ctrl Pts',(20.4891333854113,-17.7682788337557,
11.2135814277499));
#176572=CARTESIAN_POINT('Ctrl Pts',(20.4483806016486,-17.7078536480194,
11.2091941840902));
#176573=CARTESIAN_POINT('Ctrl Pts',(20.4045556257396,-17.6496122391306,
11.2048069404305));
#176574=CARTESIAN_POINT('Ctrl Pts',(20.3579349545348,-17.5938673616175,
11.2004196967708));
#176575=CARTESIAN_POINT('Ctrl Pts',(20.3262373904725,-17.5559662164717,
11.1974367938359));
#176576=CARTESIAN_POINT('Ctrl Pts',(20.2932482928822,-17.5192184270685,
11.1944538909011));
#176577=CARTESIAN_POINT('Ctrl Pts',(20.2590638380205,-17.4837121229261,
11.1914709879662));
#176578=CARTESIAN_POINT('Ctrl Pts',(20.2087743940131,-17.4314780796656,
11.1870827790353));
#176579=CARTESIAN_POINT('Ctrl Pts',(20.1557001261014,-17.3817287153967,
11.1826945701045));
#176580=CARTESIAN_POINT('Ctrl Pts',(20.1001163804879,-17.3347755149755,
11.1783063611736));
#176581=CARTESIAN_POINT('Ctrl Pts',(20.0446151303687,-17.2878920008886,
11.1739246650723));
#176582=CARTESIAN_POINT('Ctrl Pts',(19.9866121616042,-17.2437967211,11.169542968971));
#176583=CARTESIAN_POINT('Ctrl Pts',(19.9264202255137,-17.2027650227068,
11.1651612728698));
#176584=CARTESIAN_POINT('Ctrl Pts',(19.8662990197384,-17.1617815398247,
11.1607847256101));
#176585=CARTESIAN_POINT('Ctrl Pts',(19.8039943529514,-17.1238547573654,
11.1564081783505));
#176586=CARTESIAN_POINT('Ctrl Pts',(19.7398513412539,-17.0892192616151,
11.1520316310908));
#176587=CARTESIAN_POINT('Ctrl Pts',(19.675749008122,-17.0546057311928,11.1476578593739));
#176588=CARTESIAN_POINT('Ctrl Pts',(19.6098110666878,-17.0232795746615,
11.1432840876569));
#176589=CARTESIAN_POINT('Ctrl Pts',(19.5424096422235,-16.9954308470284,
11.1389103159399));
#176590=CARTESIAN_POINT('Ctrl Pts',(19.4750287282391,-16.9675905938566,
11.1345378751763));
#176591=CARTESIAN_POINT('Ctrl Pts',(19.4061856609216,-16.9432258528359,
11.1301654344128));
#176592=CARTESIAN_POINT('Ctrl Pts',(19.3362735429412,-16.9224789778194,
11.1257929936492));
#176593=CARTESIAN_POINT('Ctrl Pts',(19.2663596373004,-16.901731572303,11.1214204410819));
#176594=CARTESIAN_POINT('Ctrl Pts',(19.1953770897379,-16.8846023517757,
11.1170478885146));
#176595=CARTESIAN_POINT('Ctrl Pts',(19.1237335771408,-16.8711836364424,
11.1126753359472));
#176596=CARTESIAN_POINT('Ctrl Pts',(19.0520157102038,-16.8577509946602,
11.1082982453799));
#176597=CARTESIAN_POINT('Ctrl Pts',(18.9796359837852,-16.8480366356522,
11.1039211548126));
#176598=CARTESIAN_POINT('Ctrl Pts',(18.9070108440333,-16.8420814594286,
11.0995440642452));
#176599=CARTESIAN_POINT('Ctrl Pts',(18.834346040997,-16.8361230308623,11.0951645831863));
#176600=CARTESIAN_POINT('Ctrl Pts',(18.7614360402697,-16.833927887168,11.0907851021274));
#176601=CARTESIAN_POINT('Ctrl Pts',(18.6886982399084,-16.8354847625088,
11.0864056210684));
#176602=CARTESIAN_POINT('Ctrl Pts',(18.6158315122841,-16.8370443974006,
11.0820183774087));
#176603=CARTESIAN_POINT('Ctrl Pts',(18.5431380760581,-16.8423692966915,
11.077631133749));
#176604=CARTESIAN_POINT('Ctrl Pts',(18.4710305707955,-16.851396258381,11.0732438900893));
#176605=CARTESIAN_POINT('Ctrl Pts',(18.4220044154797,-16.8575337224938,
11.0702609871544));
#176606=CARTESIAN_POINT('Ctrl Pts',(18.373248967218,-16.8653814515023,11.0672780842196));
#176607=CARTESIAN_POINT('Ctrl Pts',(18.3248903873721,-16.8749062792316,
11.0642951812848));
#176608=CARTESIAN_POINT('Ctrl Pts',(18.2537491009801,-16.8889184462449,
11.0599069723539));
#176609=CARTESIAN_POINT('Ctrl Pts',(18.1831896640499,-16.9066171190663,
11.055518763423));
#176610=CARTESIAN_POINT('Ctrl Pts',(18.1136230257292,-16.9279393759587,
11.0511305544921));
#176611=CARTESIAN_POINT('Ctrl Pts',(18.0441596358342,-16.9492299870865,
11.0467488583908));
#176612=CARTESIAN_POINT('Ctrl Pts',(17.9756865768825,-16.9741333660322,
11.0423671622896));
#176613=CARTESIAN_POINT('Ctrl Pts',(17.9086046585656,-17.0025355785913,
11.0379854661883));
#176614=CARTESIAN_POINT('Ctrl Pts',(17.8416015668411,-17.0309044162904,
11.0336089189287));
#176615=CARTESIAN_POINT('Ctrl Pts',(17.775986810406,-17.062763733124,11.029232371669));
#176616=CARTESIAN_POINT('Ctrl Pts',(17.7121444440025,-17.0979503181745,
11.0248558244094));
#176617=CARTESIAN_POINT('Ctrl Pts',(17.6483425655001,-17.1331145884041,
11.0204820526924));
#176618=CARTESIAN_POINT('Ctrl Pts',(17.5863112682427,-17.171601707862,11.0161082809754));
#176619=CARTESIAN_POINT('Ctrl Pts',(17.5264117827666,-17.2132016512548,
11.0117345092585));
#176620=CARTESIAN_POINT('Ctrl Pts',(17.466530524905,-17.2547889356452,11.0073620684949));
#176621=CARTESIAN_POINT('Ctrl Pts',(17.4087801868835,-17.299486888407,11.0029896277313));
#176622=CARTESIAN_POINT('Ctrl Pts',(17.3534932447841,-17.3470420258451,
10.9986171869678));
#176623=CARTESIAN_POINT('Ctrl Pts',(17.2982048889918,-17.3945983792732,
10.9942446344004));
#176624=CARTESIAN_POINT('Ctrl Pts',(17.2453804185812,-17.4450117463514,
10.9898720818331));
#176625=CARTESIAN_POINT('Ctrl Pts',(17.1953181280015,-17.49798930651,10.9854995292658));
#176626=CARTESIAN_POINT('Ctrl Pts',(17.1452038808882,-17.551021848779,10.9811224386984));
#176627=CARTESIAN_POINT('Ctrl Pts',(17.0978578691728,-17.6066235460734,
10.9767453481311));
#176628=CARTESIAN_POINT('Ctrl Pts',(17.0535398976928,-17.6644663714863,
10.9723682575638));
#176629=CARTESIAN_POINT('Ctrl Pts',(17.0091977225237,-17.722340787013,10.9679887765048));
#176630=CARTESIAN_POINT('Ctrl Pts',(16.9678871535196,-17.7824583697196,
10.9636092954459));
#176631=CARTESIAN_POINT('Ctrl Pts',(16.9298246475461,-17.8444620559106,
10.9592298143869));
#176632=CARTESIAN_POINT('Ctrl Pts',(16.8916946760363,-17.9065756432192,
10.9548425707272));
#176633=CARTESIAN_POINT('Ctrl Pts',(16.8568244953673,-17.970581586091,10.9504553270675));
#176634=CARTESIAN_POINT('Ctrl Pts',(16.8253843166288,-18.0360987099094,
10.9460680834078));
#176635=CARTESIAN_POINT('Ctrl Pts',(16.8040080246551,-18.0806440408907,
10.943085180473));
#176636=CARTESIAN_POINT('Ctrl Pts',(16.7842163233974,-18.1258874840301,
10.9401022775381));
#176637=CARTESIAN_POINT('Ctrl Pts',(16.7660496141036,-18.1717050053665,
10.9371193746033));
#176638=CARTESIAN_POINT('Ctrl Pts',(16.7589277836804,-18.1896666852772,
10.9359499977764));
#176639=CARTESIAN_POINT('Ctrl Pts',(16.7520500909108,-18.2077303660208,
10.9347806209494));
#176640=CARTESIAN_POINT('Ctrl Pts',(16.7454193692319,-18.2258897639242,
10.9336112441224));
#176641=CARTESIAN_POINT('Ctrl Pts',(16.7460270540486,-18.2261211809509,
11.7337477306398));
#176642=CARTESIAN_POINT('Ctrl Pts',(16.6804602716594,-18.4003673855785,
11.7225565586572));
#176643=CARTESIAN_POINT('Ctrl Pts',(16.6235839437207,-18.6428895340021,
11.7076594081181));
#176644=CARTESIAN_POINT('Ctrl Pts',(16.6137960417384,-18.8895339291486,
11.692762257579));
#176645=CARTESIAN_POINT('Ctrl Pts',(16.6141771461173,-18.9509225630941,
11.6890562790225));
#176646=CARTESIAN_POINT('Origin',(18.734,-18.952,0.));
#176647=CARTESIAN_POINT('',(16.745419233475,-18.2258901357187,12.7565301047573));
#176648=CARTESIAN_POINT('',(16.7454193796745,-18.2258897353253,12.5316746168857));
#176649=CARTESIAN_POINT('',(16.7454193692319,-18.2258897639242,0.));
#176650=CARTESIAN_POINT('',(16.6170000980012,-18.9513558437923,12.7090269898315));
#176651=CARTESIAN_POINT('Ctrl Pts',(16.745419233475,-18.2258901357186,12.7565301047573));
#176652=CARTESIAN_POINT('Ctrl Pts',(16.7109376370553,-18.3203241088848,
12.749989613753));
#176653=CARTESIAN_POINT('Ctrl Pts',(16.6831993464591,-18.4171689088752,
12.7433091961978));
#176654=CARTESIAN_POINT('Ctrl Pts',(16.6461463540984,-18.5930957097835,
12.7314611488217));
#176655=CARTESIAN_POINT('Ctrl Pts',(16.6341942133272,-18.6713528334904,
12.726291292972));
#176656=CARTESIAN_POINT('Ctrl Pts',(16.6241532254521,-18.7761570463455,
12.7196400447783));
#176657=CARTESIAN_POINT('Ctrl Pts',(16.6221401935253,-18.802258693066,12.7180060431816));
#176658=CARTESIAN_POINT('Ctrl Pts',(16.6202046975953,-18.8353509206357,
12.715968455308));
#176659=CARTESIAN_POINT('Ctrl Pts',(16.6198320660307,-18.8423116310697,
12.7155417679485));
#176660=CARTESIAN_POINT('Ctrl Pts',(16.6192953233298,-18.8533599303491,
12.7148676711254));
#176661=CARTESIAN_POINT('Ctrl Pts',(16.6191086714274,-18.8574463017393,
12.7146190317843));
#176662=CARTESIAN_POINT('Ctrl Pts',(16.6187836658968,-18.8650447622431,
12.7141580017202));
#176663=CARTESIAN_POINT('Ctrl Pts',(16.6186422157767,-18.8685566158062,
12.7139454452355));
#176664=CARTESIAN_POINT('Ctrl Pts',(16.6183781730859,-18.8755448805823,
12.7135235017923));
#176665=CARTESIAN_POINT('Ctrl Pts',(16.618255403301,-18.8790212240566,12.7133141063902));
#176666=CARTESIAN_POINT('Ctrl Pts',(16.617993747079,-18.8869868464393,12.7128354206365));
#176667=CARTESIAN_POINT('Ctrl Pts',(16.6178605771841,-18.8914763139796,
12.7125664446215));
#176668=CARTESIAN_POINT('Ctrl Pts',(16.6175253047138,-18.9041387314715,
12.7118100153744));
#176669=CARTESIAN_POINT('Ctrl Pts',(16.617356253433,-18.9123125754478,12.7113243212429));
#176670=CARTESIAN_POINT('Ctrl Pts',(16.6170813858838,-18.9307759513804,
12.7102326704046));
#176671=CARTESIAN_POINT('Ctrl Pts',(16.6170032290559,-18.9410657272419,
12.70962810903));
#176672=CARTESIAN_POINT('Ctrl Pts',(16.6170000980012,-18.9513558437923,
12.7090269898315));
#176673=CARTESIAN_POINT('Ctrl Pts',(16.6170000985844,-18.951353930096,12.7090271016242));
#176674=CARTESIAN_POINT('Ctrl Pts',(16.6169387584984,-19.1523491399336,
12.6972855275493));
#176675=CARTESIAN_POINT('Ctrl Pts',(16.6455011370249,-19.3523727029926,
12.6868409881406));
#176676=CARTESIAN_POINT('Ctrl Pts',(16.7265430572823,-19.6299053113378,
12.6708783895896));
#176677=CARTESIAN_POINT('Ctrl Pts',(16.7564635988091,-19.7127800125277,
12.6659221852056));
#176678=CARTESIAN_POINT('Ctrl Pts',(16.7995999890664,-19.8123520374021,
12.659597526166));
#176679=CARTESIAN_POINT('Ctrl Pts',(16.8080194228569,-19.8310379989043,
12.6583942005727));
#176680=CARTESIAN_POINT('Ctrl Pts',(16.8204635507149,-19.8576189527489,
12.656657572754));
#176681=CARTESIAN_POINT('Ctrl Pts',(16.8242687401447,-19.8656158611914,
12.6561318418787));
#176682=CARTESIAN_POINT('Ctrl Pts',(16.8309531565167,-19.8794394583158,
12.6552172779321));
#176683=CARTESIAN_POINT('Ctrl Pts',(16.8338092647821,-19.8852772394481,
12.6548292530634));
#176684=CARTESIAN_POINT('Ctrl Pts',(16.839353145055,-19.8964777804216,12.6540812698207));
#176685=CARTESIAN_POINT('Ctrl Pts',(16.8420369216835,-19.9018424563047,
12.6537214541484));
#176686=CARTESIAN_POINT('Ctrl Pts',(16.8491287513787,-19.915869201835,12.6527765353977));
#176687=CARTESIAN_POINT('Ctrl Pts',(16.8535736818294,-19.9245123747944,
12.6521901394028));
#176688=CARTESIAN_POINT('Ctrl Pts',(16.8692145486086,-19.9544179033586,
12.6501465724257));
#176689=CARTESIAN_POINT('Ctrl Pts',(16.8807125432645,-19.9755193993012,
12.6486787523838));
#176690=CARTESIAN_POINT('Ctrl Pts',(16.9644713381321,-20.1231958391753,
12.6382181144485));
#176691=CARTESIAN_POINT('Ctrl Pts',(17.0492628607079,-20.2421853723023,
12.628759163819));
#176692=CARTESIAN_POINT('Ctrl Pts',(17.2361826289279,-20.454336360999,12.6100989798091));
#176693=CARTESIAN_POINT('Ctrl Pts',(17.3365605456481,-20.5481328257092,
12.6009691548132));
#176694=CARTESIAN_POINT('Ctrl Pts',(17.4553919521303,-20.6393091050874,
12.5915893604774));
#176695=CARTESIAN_POINT('Ctrl Pts',(17.4655458525329,-20.646955648069,12.5907984450836));
#176696=CARTESIAN_POINT('Ctrl Pts',(17.4811882495519,-20.6585160822712,
12.5895968554965));
#176697=CARTESIAN_POINT('Ctrl Pts',(17.4866274100139,-20.6624958478733,
12.5891821130145));
#176698=CARTESIAN_POINT('Ctrl Pts',(17.4956204221168,-20.6690102133911,
12.5885015577888));
#176699=CARTESIAN_POINT('Ctrl Pts',(17.4991632266578,-20.6715598843255,
12.5882347646989));
#176700=CARTESIAN_POINT('Ctrl Pts',(17.5060264636832,-20.6764670412889,
12.5877204959167));
#176701=CARTESIAN_POINT('Ctrl Pts',(17.5093458592576,-20.6788259375495,
12.5874729258201));
#176702=CARTESIAN_POINT('Ctrl Pts',(17.5126817605774,-20.6811821067182,
12.5872252982733));
#176703=CARTESIAN_POINT('Ctrl Pts',(17.512691448454,-20.6811889492075,12.5872245791417));
#176704=CARTESIAN_POINT('Ctrl Pts',(17.512710858349,-20.6812026580558,12.587223138364));
#176705=CARTESIAN_POINT('Ctrl Pts',(17.5127205805917,-20.6812095245722,
12.5872224167013));
#176706=CARTESIAN_POINT('Ctrl Pts',(17.5127400599372,-20.6812232819797,
12.5872209708083));
#176707=CARTESIAN_POINT('Ctrl Pts',(17.5127498165402,-20.6812301725167,
12.5872202466152));
#176708=CARTESIAN_POINT('Ctrl Pts',(17.5127699763166,-20.6812444099712,
12.5872187502574));
#176709=CARTESIAN_POINT('Ctrl Pts',(17.5127803797835,-20.6812517570789,
12.5872179780724));
#176710=CARTESIAN_POINT('Ctrl Pts',(17.51280135382,-20.6812665690216,12.5872164213223));
#176711=CARTESIAN_POINT('Ctrl Pts',(17.5128119249259,-20.6812740342306,
12.5872156367178));
#176712=CARTESIAN_POINT('Ctrl Pts',(17.5128332384424,-20.6812890853295,
12.5872140548181));
#176713=CARTESIAN_POINT('Ctrl Pts',(17.5128439802992,-20.6812966708236,
12.5872132575644));
#176714=CARTESIAN_POINT('Ctrl Pts',(17.5128656391579,-20.68131196519,12.5872116500824));
#176715=CARTESIAN_POINT('Ctrl Pts',(17.5128765558774,-20.6813196738581,
12.5872108398754));
#176716=CARTESIAN_POINT('Ctrl Pts',(17.5128985675731,-20.6813352167551,
12.5872092062572));
#176717=CARTESIAN_POINT('Ctrl Pts',(17.5129096631058,-20.6813430513719,
12.587208382805));
#176718=CARTESIAN_POINT('Ctrl Pts',(17.5129320361737,-20.6813588487956,
12.5872067224197));
#176719=CARTESIAN_POINT('Ctrl Pts',(17.5129433140281,-20.6813668118228,
12.5872058854632));
#176720=CARTESIAN_POINT('Ctrl Pts',(17.5129660562625,-20.6813828692449,
12.5872041977348));
#176721=CARTESIAN_POINT('Ctrl Pts',(17.5129775202629,-20.6813909633665,
12.5872033469915));
#176722=CARTESIAN_POINT('Ctrl Pts',(17.5158229631571,-20.6833999370059,
12.5869921901589));
#176723=CARTESIAN_POINT('Ctrl Pts',(17.5186618181092,-20.6853938210381,
12.5867823736062));
#176724=CARTESIAN_POINT('Ctrl Pts',(17.525220924777,-20.6899766077734,12.5862995428218));
#176725=CARTESIAN_POINT('Ctrl Pts',(17.5289445907593,-20.6925605428716,
12.5860268688936));
#176726=CARTESIAN_POINT('Ctrl Pts',(17.5402942394825,-20.7003824375166,
12.5852000211581));
#176727=CARTESIAN_POINT('Ctrl Pts',(17.5479464019355,-20.7055824645766,
12.5846483616946));
#176728=CARTESIAN_POINT('Ctrl Pts',(17.6100857169512,-20.7472163998169,
12.5802133160385));
#176729=CARTESIAN_POINT('Ctrl Pts',(17.6662097271447,-20.781155800408,12.5764835169958));
#176730=CARTESIAN_POINT('Ctrl Pts',(17.8585115394434,-20.8855713347812,
12.5642916148332));
#176731=CARTESIAN_POINT('Ctrl Pts',(18.0007454983207,-20.9438635182883,
12.5561801606446));
#176732=CARTESIAN_POINT('Ctrl Pts',(18.2068817673174,-21.0032400936249,
12.5443080186182));
#176733=CARTESIAN_POINT('Ctrl Pts',(18.2664347852464,-21.0176285926644,
12.540870094101));
#176734=CARTESIAN_POINT('Ctrl Pts',(18.362847280636,-21.0365394573643,12.5352306100049));
#176735=CARTESIAN_POINT('Ctrl Pts',(18.3993487191498,-21.0427097755614,
12.533079160296));
#176736=CARTESIAN_POINT('Ctrl Pts',(18.4469898674044,-21.0494836331061,
12.5302424811072));
#176737=CARTESIAN_POINT('Ctrl Pts',(18.4580001124448,-21.0509608053313,
12.5295849394513));
#176738=CARTESIAN_POINT('Ctrl Pts',(18.4759307960182,-21.0532229264647,
12.5285107194485));
#176739=CARTESIAN_POINT('Ctrl Pts',(18.4828444693868,-21.0540605125461,
12.5280957078072));
#176740=CARTESIAN_POINT('Ctrl Pts',(18.4961518778526,-21.0556061064271,
12.5272952759627));
#176741=CARTESIAN_POINT('Ctrl Pts',(18.5025449627141,-21.056319116604,12.5269100183782));
#176742=CARTESIAN_POINT('Ctrl Pts',(18.5171959173523,-21.0578855405652,
12.5260254427567));
#176743=CARTESIAN_POINT('Ctrl Pts',(18.5254557174255,-21.0587195350482,
12.5255255184606));
#176744=CARTESIAN_POINT('Ctrl Pts',(18.5474242848536,-21.0608072464684,
12.5241925233397));
#176745=CARTESIAN_POINT('Ctrl Pts',(18.5611405658324,-21.0619758534661,
12.5233567920771));
#176746=CARTESIAN_POINT('Ctrl Pts',(18.666550141721,-21.069921877109,12.5169066518896));
#176747=CARTESIAN_POINT('Ctrl Pts',(18.7585737897712,-21.0708522280832,
12.5111091269597));
#176748=CARTESIAN_POINT('Ctrl Pts',(18.9909055698545,-21.0580632370058,
12.4960736927044));
#176749=CARTESIAN_POINT('Ctrl Pts',(19.1303286609935,-21.0363276217036,
12.4866630167631));
#176750=CARTESIAN_POINT('Ctrl Pts',(19.3179759046464,-20.9875551404384,
12.4739796095789));
#176751=CARTESIAN_POINT('Ctrl Pts',(19.3688867110647,-20.9722554831229,
12.4705406573022));
#176752=CARTESIAN_POINT('Ctrl Pts',(19.4454171487295,-20.9460772571932,
12.4654251230767));
#176753=CARTESIAN_POINT('Ctrl Pts',(19.471485893641,-20.9365838846983,12.4636924881725));
#176754=CARTESIAN_POINT('Ctrl Pts',(19.50378263953,-20.9240981403221,12.4615648784054));
#176755=CARTESIAN_POINT('Ctrl Pts',(19.5101913265726,-20.9215845792313,
12.4611436376714));
#176756=CARTESIAN_POINT('Ctrl Pts',(19.5203332228452,-20.9175496207974,
12.4604786444813));
#176757=CARTESIAN_POINT('Ctrl Pts',(19.5240744783274,-20.9160487693766,
12.4602336875952));
#176758=CARTESIAN_POINT('Ctrl Pts',(19.531136059079,-20.9131924853526,12.4597720337456));
#176759=CARTESIAN_POINT('Ctrl Pts',(19.5344571854397,-20.9118393188562,
12.4595552110787));
#176760=CARTESIAN_POINT('Ctrl Pts',(19.5420600916517,-20.908719025256,12.4590595086698));
#176761=CARTESIAN_POINT('Ctrl Pts',(19.5463395171316,-20.9069462819625,
12.4587809723338));
#176762=CARTESIAN_POINT('Ctrl Pts',(19.5577219916981,-20.9021872859304,
12.458041305005));
#176763=CARTESIAN_POINT('Ctrl Pts',(19.5648146896711,-20.8991762440327,
12.4575816355015));
#176764=CARTESIAN_POINT('Ctrl Pts',(19.6153759309035,-20.8773850670431,
12.454312580212));
#176765=CARTESIAN_POINT('Ctrl Pts',(19.6582235658535,-20.8571883700647,
12.4515832835482));
#176766=CARTESIAN_POINT('Ctrl Pts',(19.8433928338141,-20.7621877190933,
12.4398180639204));
#176767=CARTESIAN_POINT('Ctrl Pts',(19.9776098584288,-20.6727483314295,
12.4313328864275));
#176768=CARTESIAN_POINT('Ctrl Pts',(20.1719595324536,-20.5085136753798,
12.4173245874353));
#176769=CARTESIAN_POINT('Ctrl Pts',(20.2394035446849,-20.4433817956119,
12.4120677355598));
#176770=CARTESIAN_POINT('Ctrl Pts',(20.3165393595728,-20.3583096967044,
12.4053794477549));
#176771=CARTESIAN_POINT('Ctrl Pts',(20.330532436469,-20.3424035094087,12.4041362151558));
#176772=CARTESIAN_POINT('Ctrl Pts',(20.3501102097249,-20.3194638335095,
12.4023521424112));
#176773=CARTESIAN_POINT('Ctrl Pts',(20.355892791097,-20.3126003514418,12.4018194635633));
#176774=CARTESIAN_POINT('Ctrl Pts',(20.3658006983028,-20.3006875072799,
12.4008967038198));
#176775=CARTESIAN_POINT('Ctrl Pts',(20.3699466909577,-20.2956554372874,
12.4005074719962));
#176776=CARTESIAN_POINT('Ctrl Pts',(20.3778456198546,-20.2859776029158,
12.3997598964505));
#176777=CARTESIAN_POINT('Ctrl Pts',(20.3816022779119,-20.2813349463847,
12.3994017085141));
#176778=CARTESIAN_POINT('Ctrl Pts',(20.3913309177388,-20.2692072423718,
12.3984671406283));
#176779=CARTESIAN_POINT('Ctrl Pts',(20.3972718000627,-20.2616975241075,
12.3978895221537));
#176780=CARTESIAN_POINT('Ctrl Pts',(20.4174127358698,-20.235879815631,12.3959072370737));
#176781=CARTESIAN_POINT('Ctrl Pts',(20.4313626889712,-20.217379648732,12.3944927539433));
#176782=CARTESIAN_POINT('Ctrl Pts',(20.5468826537919,-20.0588310872862,
12.3824160627589));
#176783=CARTESIAN_POINT('Ctrl Pts',(20.6312175552133,-19.9070715305983,
12.371072494265));
#176784=CARTESIAN_POINT('Ctrl Pts',(20.7294681025797,-19.6645133292593,
12.3537798377189));
#176785=CARTESIAN_POINT('Ctrl Pts',(20.7575877815373,-19.5802218108695,
12.3479253459652));
#176786=CARTESIAN_POINT('Ctrl Pts',(20.7901372059195,-19.4574234435621,
12.339811425075));
#176787=CARTESIAN_POINT('Ctrl Pts',(20.798937023073,-19.4201758014434,12.3374038693267));
#176788=CARTESIAN_POINT('Ctrl Pts',(20.8082684141023,-19.3752697202377,
12.334581364908));
#176789=CARTESIAN_POINT('Ctrl Pts',(20.8097739569206,-19.3678235125622,
12.3341159650303));
#176790=CARTESIAN_POINT('Ctrl Pts',(20.8120472110773,-19.3562602195026,
12.3333974730016));
#176791=CARTESIAN_POINT('Ctrl Pts',(20.8128428257087,-19.3521487763807,
12.3331428341966));
#176792=CARTESIAN_POINT('Ctrl Pts',(20.8142928397379,-19.344534581819,12.3326728219506));
#176793=CARTESIAN_POINT('Ctrl Pts',(20.8149505899459,-19.3410325686837,
12.3324572643964));
#176794=CARTESIAN_POINT('Ctrl Pts',(20.8164140859918,-19.3331306624519,
12.3319722599344));
#176795=CARTESIAN_POINT('Ctrl Pts',(20.8172147287858,-19.3287298793731,
12.3317031056756));
#176796=CARTESIAN_POINT('Ctrl Pts',(20.8195267345964,-19.3157890255295,
12.3309143616869));
#176797=CARTESIAN_POINT('Ctrl Pts',(20.820999594904,-19.3072420477756,12.3303969084771));
#176798=CARTESIAN_POINT('Ctrl Pts',(20.8309784506855,-19.247129913356,12.3267805164844));
#176799=CARTESIAN_POINT('Ctrl Pts',(20.8376256911425,-19.1952698181811,
12.3237788397212));
#176800=CARTESIAN_POINT('Ctrl Pts',(20.8557089524903,-18.99588020985,12.3125092756898));
#176801=CARTESIAN_POINT('Ctrl Pts',(20.8535918344382,-18.8475449365391,
12.3046645302514));
#176802=CARTESIAN_POINT('Ctrl Pts',(20.8272110131162,-18.6269377144654,
12.2924688625413));
#176803=CARTESIAN_POINT('Ctrl Pts',(20.8145292331848,-18.5537605871344,
12.288339082253));
#176804=CARTESIAN_POINT('Ctrl Pts',(20.7886214857222,-18.4401291292198,
12.2816783201896));
#176805=CARTESIAN_POINT('Ctrl Pts',(20.7779752625796,-18.3991473947878,
12.2792246775098));
#176806=CARTESIAN_POINT('Ctrl Pts',(20.762844837689,-18.3473404860542,12.2760455634214));
#176807=CARTESIAN_POINT('Ctrl Pts',(20.7594894287573,-18.3361939680028,
12.2753569542095));
#176808=CARTESIAN_POINT('Ctrl Pts',(20.7539450662766,-18.3183115246201,
12.2742445632182));
#176809=CARTESIAN_POINT('Ctrl Pts',(20.7518139095322,-18.3115578252244,
12.2738226795348));
#176810=CARTESIAN_POINT('Ctrl Pts',(20.7476922206989,-18.2987208809542,
12.2730173763892));
#176811=CARTESIAN_POINT('Ctrl Pts',(20.7457079062284,-18.2926357109243,
12.2726341654605));
#176812=CARTESIAN_POINT('Ctrl Pts',(20.7411175449446,-18.2787723625611,
12.2717577299614));
#176813=CARTESIAN_POINT('Ctrl Pts',(20.7384938348935,-18.2710001806513,
12.2712639260701));
#176814=CARTESIAN_POINT('Ctrl Pts',(20.7315513730298,-18.2508223752519,
12.2699754606284));
#176815=CARTESIAN_POINT('Ctrl Pts',(20.7271622603064,-18.2384414941896,
12.2691784769792));
#176816=CARTESIAN_POINT('Ctrl Pts',(20.6968874511393,-18.1555010677523,
12.2637955428458));
#176817=CARTESIAN_POINT('Ctrl Pts',(20.6673780879971,-18.0863299267917,
12.2590888855984));
#176818=CARTESIAN_POINT('Ctrl Pts',(20.5478302745639,-17.8428761851375,
12.241723105962));
#176819=CARTESIAN_POINT('Ctrl Pts',(20.4373868060522,-17.6797599433705,
12.2284365607606));
#176820=CARTESIAN_POINT('Ctrl Pts',(20.2779186885959,-17.5029404374827,
12.2131811693824));
#176821=CARTESIAN_POINT('Ctrl Pts',(20.2488188000974,-17.47254635569,12.2105277724223));
#176822=CARTESIAN_POINT('Ctrl Pts',(20.2132718230554,-17.4375678664744,
12.2074575205682));
#176823=CARTESIAN_POINT('Ctrl Pts',(20.2076830418903,-17.4321289166766,
12.2069796221389));
#176824=CARTESIAN_POINT('Ctrl Pts',(20.1990156959125,-17.4237866923221,
12.206246045626));
#176825=CARTESIAN_POINT('Ctrl Pts',(20.195958336003,-17.4208616236448,12.2059887175285));
#176826=CARTESIAN_POINT('Ctrl Pts',(20.190312161353,-17.415492087379,12.2055161716218));
#176827=CARTESIAN_POINT('Ctrl Pts',(20.1877259672089,-17.4130450008326,
12.2053007539933));
#176828=CARTESIAN_POINT('Ctrl Pts',(20.1819157175426,-17.4075749915894,
12.2048190797231));
#176829=CARTESIAN_POINT('Ctrl Pts',(20.1786883732793,-17.4045556434437,
12.2045530975841));
#176830=CARTESIAN_POINT('Ctrl Pts',(20.170442699461,-17.3968896679103,12.203877436766));
#176831=CARTESIAN_POINT('Ctrl Pts',(20.1654112213633,-17.3922571711833,
12.2034688138349));
#176832=CARTESIAN_POINT('Ctrl Pts',(20.1365546941091,-17.365946119365,12.201145493204));
#176833=CARTESIAN_POINT('Ctrl Pts',(20.1122583785761,-17.3447879177703,
12.1992674936093));
#176834=CARTESIAN_POINT('Ctrl Pts',(20.0726371808267,-17.3118437632991,
12.1963097891391));
#176835=CARTESIAN_POINT('Ctrl Pts',(20.0576184774976,-17.2996997396068,
12.1952117566252));
#176836=CARTESIAN_POINT('Ctrl Pts',(20.0412973964723,-17.2868679895253,
12.1940405545374));
#176837=CARTESIAN_POINT('Ctrl Pts',(20.0401585879162,-17.2859745385022,
12.1939589475208));
#176838=CARTESIAN_POINT('Ctrl Pts',(20.0209801434389,-17.2709598613527,
12.1925865202655));
#176839=CARTESIAN_POINT('Ctrl Pts',(20.0027129111959,-17.257130849011,12.1913075521928));
#176840=CARTESIAN_POINT('Ctrl Pts',(19.9473633596232,-17.2166254707547,
12.1875044452394));
#176841=CARTESIAN_POINT('Ctrl Pts',(19.9096378810851,-17.190849464661,12.185006783572));
#176842=CARTESIAN_POINT('Ctrl Pts',(19.7788706322771,-17.1075782042713,
12.176566325358));
#176843=CARTESIAN_POINT('Ctrl Pts',(19.6822228443343,-17.0560783369137,
12.1706782295262));
#176844=CARTESIAN_POINT('Ctrl Pts',(19.5315382449814,-16.9902000913379,
12.1615338802592));
#176845=CARTESIAN_POINT('Ctrl Pts',(19.480203254375,-16.9701054035043,12.1584263564109));
#176846=CARTESIAN_POINT('Ctrl Pts',(19.3957343068887,-16.9407879958885,
12.1532823340521));
#176847=CARTESIAN_POINT('Ctrl Pts',(19.3630560922159,-16.9303288460667,
12.1512852234229));
#176848=CARTESIAN_POINT('Ctrl Pts',(19.3197679542108,-16.9176249764081,
12.1486245776851));
#176849=CARTESIAN_POINT('Ctrl Pts',(19.3093734276155,-16.9146607437567,
12.1479845708699));
#176850=CARTESIAN_POINT('Ctrl Pts',(19.2923087968333,-16.9099353898033,
12.14693186345));
#176851=CARTESIAN_POINT('Ctrl Pts',(19.2856518967962,-16.9081270176773,
12.146520704133));
#176852=CARTESIAN_POINT('Ctrl Pts',(19.2727471251941,-16.904689025628,12.14572263557));
#176853=CARTESIAN_POINT('Ctrl Pts',(19.2665003956321,-16.9030553892533,
12.1453358617018));
#176854=CARTESIAN_POINT('Ctrl Pts',(19.2520570053359,-16.8993486848564,
12.1444404822383));
#176855=CARTESIAN_POINT('Ctrl Pts',(19.2438552449605,-16.8972961020417,
12.1439312205101));
#176856=CARTESIAN_POINT('Ctrl Pts',(19.2217585252902,-16.8919065982599,
12.1425569070159));
#176857=CARTESIAN_POINT('Ctrl Pts',(19.2078418963296,-16.888661190097,12.1416889271498));
#176858=CARTESIAN_POINT('Ctrl Pts',(19.0798346869732,-16.8601727615451,
12.1336815866335));
#176859=CARTESIAN_POINT('Ctrl Pts',(18.9638886762455,-16.8442793791146,
12.1262404422541));
#176860=CARTESIAN_POINT('Ctrl Pts',(18.6847501670076,-16.8293266673691,
12.1079811209209));
#176861=CARTESIAN_POINT('Ctrl Pts',(18.5218032703257,-16.8393854483171,
12.0970228893712));
#176862=CARTESIAN_POINT('Ctrl Pts',(18.3296149874438,-16.8737270062533,
12.0846173736403));
#176863=CARTESIAN_POINT('Ctrl Pts',(18.2977461474967,-16.8801822667745,
12.0825798128478));
#176864=CARTESIAN_POINT('Ctrl Pts',(18.2589760673537,-16.8889697827556,
12.0801352602503));
#176865=CARTESIAN_POINT('Ctrl Pts',(18.2519235576139,-16.8906063643655,
12.0796919792357));
#176866=CARTESIAN_POINT('Ctrl Pts',(18.2408809623921,-16.8932286420363,
12.0790002480952));
#176867=CARTESIAN_POINT('Ctrl Pts',(18.2368851928136,-16.8941898146907,
12.0787504271908));
#176868=CARTESIAN_POINT('Ctrl Pts',(18.2294218356467,-16.8960081142196,
12.0782847434123));
#176869=CARTESIAN_POINT('Ctrl Pts',(18.2259536565098,-16.8968623716565,
12.0780687250689));
#176870=CARTESIAN_POINT('Ctrl Pts',(18.2180420208525,-16.8988323614393,
12.0775767986321));
#176871=CARTESIAN_POINT('Ctrl Pts',(18.2136000222378,-16.8999537402073,
12.0773012197026));
#176872=CARTESIAN_POINT('Ctrl Pts',(18.1999589389986,-16.903444562333,12.0764567249938));
#176873=CARTESIAN_POINT('Ctrl Pts',(18.1907719880553,-16.9058615465525,
12.0758904833148));
#176874=CARTESIAN_POINT('Ctrl Pts',(18.1084481485608,-16.9281135743674,
12.0708363939015));
#176875=CARTESIAN_POINT('Ctrl Pts',(18.0364006911938,-16.9518027143419,
12.0665543201682));
#176876=CARTESIAN_POINT('Ctrl Pts',(17.9259491138241,-16.9948160248289,
12.0599935301445));
#176877=CARTESIAN_POINT('Ctrl Pts',(17.8866041397313,-17.0115269160435,
12.0576573699983));
#176878=CARTESIAN_POINT('Ctrl Pts',(17.748509387532,-17.0751813046516,12.0493787639311));
#176879=CARTESIAN_POINT('Ctrl Pts',(17.652922689133,-17.1285661176162,12.0434920638108));
#176880=CARTESIAN_POINT('Ctrl Pts',(17.5160261081469,-17.2195849389946,
12.0343509592961));
#176881=CARTESIAN_POINT('Ctrl Pts',(17.4713725651031,-17.2518548117505,
12.0312452952386));
#176882=CARTESIAN_POINT('Ctrl Pts',(17.4010406323783,-17.3069819832352,
12.0261040770406));
#176883=CARTESIAN_POINT('Ctrl Pts',(17.3745704100411,-17.3287883856939,
12.0241078544905));
#176884=CARTESIAN_POINT('Ctrl Pts',(17.3404706846839,-17.3582993249946,
12.0214482242515));
#176885=CARTESIAN_POINT('Ctrl Pts',(17.3323532447383,-17.3654338459847,
12.020808321938));
#176886=CARTESIAN_POINT('Ctrl Pts',(17.3191448665736,-17.3772233393769,
12.0197557426236));
#176887=CARTESIAN_POINT('Ctrl Pts',(17.3140213605869,-17.3818416508819,
12.019344606174));
#176888=CARTESIAN_POINT('Ctrl Pts',(17.30414563728,-17.3908314651692,12.0185465506995));
#176889=CARTESIAN_POINT('Ctrl Pts',(17.2993906644587,-17.3951998375899,
12.0181597668866));
#176890=CARTESIAN_POINT('Ctrl Pts',(17.2884551786142,-17.4053388645086,
12.0172643187998));
#176891=CARTESIAN_POINT('Ctrl Pts',(17.2822891370255,-17.4111249026102,
12.0167549980764));
#176892=CARTESIAN_POINT('Ctrl Pts',(17.2657938227598,-17.4267905326563,
12.0153804221432));
#176893=CARTESIAN_POINT('Ctrl Pts',(17.2555298075458,-17.4367379195475,
12.0145122370931));
#176894=CARTESIAN_POINT('Ctrl Pts',(17.1621046109403,-17.5291340808477,
12.0064890741994));
#176895=CARTESIAN_POINT('Ctrl Pts',(17.0858314349433,-17.6182327551735,
11.9990309274255));
#176896=CARTESIAN_POINT('Ctrl Pts',(16.9216222661207,-17.8457806349321,
11.9806998371347));
#176897=CARTESIAN_POINT('Ctrl Pts',(16.8416122532993,-17.9890341906866,
11.9696846986281));
#176898=CARTESIAN_POINT('Ctrl Pts',(16.7671124263905,-18.1684279081479,
11.9573528957394));
#176899=CARTESIAN_POINT('Ctrl Pts',(16.7559529427131,-18.1970417197062,
11.9554288751158));
#176900=CARTESIAN_POINT('Ctrl Pts',(16.7454193692303,-18.2258897639288,
11.9535387439396));
#176901=CARTESIAN_POINT('',(16.6163526597653,-18.9538935158516,12.4890562790225));
#176902=CARTESIAN_POINT('Ctrl Pts',(16.6163526597653,-18.9538935158516,
12.4890562790225));
#176903=CARTESIAN_POINT('Ctrl Pts',(16.6150299521963,-19.0968822256806,
12.4804472042752));
#176904=CARTESIAN_POINT('Ctrl Pts',(16.6934796266312,-19.9425183495545,
12.4294461939675));
#176905=CARTESIAN_POINT('Ctrl Pts',(17.8308508893114,-21.2866630207328,
12.336053248099));
#176906=CARTESIAN_POINT('Ctrl Pts',(20.2082246479652,-20.9751142883798,
12.2088774414178));
#176907=CARTESIAN_POINT('Ctrl Pts',(21.2330887928116,-18.8074837650725,
12.0817016347363));
#176908=CARTESIAN_POINT('Ctrl Pts',(19.9651940811972,-16.7724379176221,
11.9545258280548));
#176909=CARTESIAN_POINT('Ctrl Pts',(17.7787242000293,-16.7401230151528,
11.8385411933561));
#176910=CARTESIAN_POINT('Ctrl Pts',(16.9288259315082,-17.7403262487167,
11.7649484942177));
#176911=CARTESIAN_POINT('Ctrl Pts',(16.7460270540486,-18.2261211809509,
11.7337477306398));
#176912=CARTESIAN_POINT('Ctrl Pts',(16.6170008641597,-18.9539128124127,
12.4894293145889));
#176913=CARTESIAN_POINT('Ctrl Pts',(16.61686182884,-18.8000359085997,12.4977958886218));
#176914=CARTESIAN_POINT('Ctrl Pts',(16.6334990646906,-18.6466112287001,
12.5060892767326));
#176915=CARTESIAN_POINT('Ctrl Pts',(16.6718564308235,-18.4725783837167,
12.5163208831024));
#176916=CARTESIAN_POINT('Ctrl Pts',(16.6775034084717,-18.4489066819874,
12.5177296503482));
#176917=CARTESIAN_POINT('Ctrl Pts',(16.686720476686,-18.4130220320893,12.5198939763803));
#176918=CARTESIAN_POINT('Ctrl Pts',(16.6899947797334,-18.4007347774334,
12.5206402325011));
#176919=CARTESIAN_POINT('Ctrl Pts',(16.6962859720509,-18.3779531736438,
12.5220338660587));
#176920=CARTESIAN_POINT('Ctrl Pts',(16.699273754911,-18.3674511831009,12.5226802921767));
#176921=CARTESIAN_POINT('Ctrl Pts',(16.7042882643285,-18.3503296679285,
12.5237408713038));
#176922=CARTESIAN_POINT('Ctrl Pts',(16.706266479128,-18.3436960587008,12.5241534375387));
#176923=CARTESIAN_POINT('Ctrl Pts',(16.7101499741267,-18.3309028720308,
12.5249523335374));
#176924=CARTESIAN_POINT('Ctrl Pts',(16.7120509309033,-18.324742054533,12.5253385178245));
#176925=CARTESIAN_POINT('Ctrl Pts',(16.7164922824257,-18.3105780534125,
12.5262297814064));
#176926=CARTESIAN_POINT('Ctrl Pts',(16.7190521956296,-18.3025811470815,
12.5267354978479));
#176927=CARTESIAN_POINT('Ctrl Pts',(16.7260350616877,-18.2812061871486,
12.528094072565));
#176928=CARTESIAN_POINT('Ctrl Pts',(16.7305440575928,-18.2678568829419,
12.5289497555122));
#176929=CARTESIAN_POINT('Ctrl Pts',(16.7385289853529,-18.2449728425729,
12.5304292889232));
#176930=CARTESIAN_POINT('Ctrl Pts',(16.7419402632179,-18.2354179074198,
12.5310508845614));
#176931=CARTESIAN_POINT('Ctrl Pts',(16.7454193796745,-18.2258897353253,
12.5316746168857));
#176932=CARTESIAN_POINT('Origin',(18.734,-18.952,0.));
#176933=CARTESIAN_POINT('',(16.7454193670368,-18.225889769936,13.5571445045843));
#176934=CARTESIAN_POINT('',(16.7454194046024,-18.225889667056,13.3344632333882));
#176935=CARTESIAN_POINT('',(16.7454193692319,-18.2258897639242,0.));
#176936=CARTESIAN_POINT('Ctrl Pts',(16.7454193670368,-18.225889769936,13.5571445045843));
#176937=CARTESIAN_POINT('Ctrl Pts',(16.7397540777375,-18.2414051615587,
13.5562052486256));
#176938=CARTESIAN_POINT('Ctrl Pts',(16.7342701807751,-18.2569873757464,
13.5552608713158));
#176939=CARTESIAN_POINT('Ctrl Pts',(16.7177768402589,-18.3056645621676,
13.5523054446821));
#176940=CARTESIAN_POINT('Ctrl Pts',(16.7074032789666,-18.338965863775,13.5502759065929));
#176941=CARTESIAN_POINT('Ctrl Pts',(16.6948809077505,-18.3829652340778,
13.5475782018768));
#176942=CARTESIAN_POINT('Ctrl Pts',(16.6919850814778,-18.393446239775,13.546934408309));
#176943=CARTESIAN_POINT('Ctrl Pts',(16.6873806776799,-18.4106257016832,
13.5458770579171));
#176944=CARTESIAN_POINT('Ctrl Pts',(16.6856239155074,-18.4173111221388,
13.5454650691535));
#176945=CARTESIAN_POINT('Ctrl Pts',(16.6822909632511,-18.4302523150924,
13.5446665179402));
#176946=CARTESIAN_POINT('Ctrl Pts',(16.6807105627383,-18.4365069315847,
13.5442800968442));
#176947=CARTESIAN_POINT('Ctrl Pts',(16.6771333675575,-18.4509415646002,
13.5433871686425));
#176948=CARTESIAN_POINT('Ctrl Pts',(16.6751567481575,-18.4591264254561,
13.5428800167108));
#176949=CARTESIAN_POINT('Ctrl Pts',(16.669984661888,-18.4811173186774,13.5415150770491));
#176950=CARTESIAN_POINT('Ctrl Pts',(16.6668789457878,-18.4949438246381,
13.5406544230393));
#176951=CARTESIAN_POINT('Ctrl Pts',(16.6325818101608,-18.6551381186332,
13.5306528456841));
#176952=CARTESIAN_POINT('Ctrl Pts',(16.61686249379,-18.80435730651,13.5210013227026));
#176953=CARTESIAN_POINT('Ctrl Pts',(16.617139475852,-19.1037302275103,13.5012717620163));
#176954=CARTESIAN_POINT('Ctrl Pts',(16.6331712118,-19.2530733037885,13.491256604518));
#176955=CARTESIAN_POINT('Ctrl Pts',(16.6681544973406,-19.414837116752,13.4809318602064));
#176956=CARTESIAN_POINT('Ctrl Pts',(16.671646380384,-19.4301562700134,13.4799597682651));
#176957=CARTESIAN_POINT('Ctrl Pts',(16.6766589549823,-19.45106952283,13.4786417997937));
#176958=CARTESIAN_POINT('Ctrl Pts',(16.6780324476134,-19.4566979190367,
13.4782880009333));
#176959=CARTESIAN_POINT('Ctrl Pts',(16.6802514660687,-19.4656317738238,
13.4777279427419));
#176960=CARTESIAN_POINT('Ctrl Pts',(16.6810818950885,-19.4689409005052,
13.4775208277027));
#176961=CARTESIAN_POINT('Ctrl Pts',(16.6828132680598,-19.4757701724302,
13.4770940975099));
#176962=CARTESIAN_POINT('Ctrl Pts',(16.683715275648,-19.4792900075426,13.476874551018));
#176963=CARTESIAN_POINT('Ctrl Pts',(16.6858857803258,-19.4876700227241,
13.4763527567906));
#176964=CARTESIAN_POINT('Ctrl Pts',(16.6871625310551,-19.4925280815868,
13.4760509848377));
#176965=CARTESIAN_POINT('Ctrl Pts',(16.6915249222324,-19.5088899472461,
13.4750369171376));
#176966=CARTESIAN_POINT('Ctrl Pts',(16.6946904139781,-19.5203724867509,
13.4743290897684));
#176967=CARTESIAN_POINT('Ctrl Pts',(16.7322349568108,-19.6522089362141,
13.466239928194));
#176968=CARTESIAN_POINT('Ctrl Pts',(16.7771311668151,-19.7693305003975,
13.4594083444331));
#176969=CARTESIAN_POINT('Ctrl Pts',(16.9057920165547,-20.0324993917894,
13.4434861959413));
#176970=CARTESIAN_POINT('Ctrl Pts',(16.9970991412317,-20.1738804480263,
13.4344327500289));
#176971=CARTESIAN_POINT('Ctrl Pts',(17.1191104086189,-20.321076989644,13.4233283615741));
#176972=CARTESIAN_POINT('Ctrl Pts',(17.1343922185398,-20.3389012497791,
13.4219533605422));
#176973=CARTESIAN_POINT('Ctrl Pts',(17.1563533934006,-20.3636702364947,
13.4199973617549));
#176974=CARTESIAN_POINT('Ctrl Pts',(17.1627888967527,-20.3708295656282,
13.4194265183191));
#176975=CARTESIAN_POINT('Ctrl Pts',(17.1733018887458,-20.3823657518555,
13.4184976394722));
#176976=CARTESIAN_POINT('Ctrl Pts',(17.1773495381483,-20.3867697087128,
13.4181408702086));
#176977=CARTESIAN_POINT('Ctrl Pts',(17.1858428983935,-20.3959324772972,
13.4173940041625));
#176978=CARTESIAN_POINT('Ctrl Pts',(17.1902920068177,-20.4006880411471,
13.4170037639558));
#176979=CARTESIAN_POINT('Ctrl Pts',(17.2008948582338,-20.4119169140896,
13.4160760657506));
#176980=CARTESIAN_POINT('Ctrl Pts',(17.2070677277317,-20.4183719186616,
13.4155377839533));
#176981=CARTESIAN_POINT('Ctrl Pts',(17.2278430690836,-20.4398233843199,
13.4137320316772));
#176982=CARTESIAN_POINT('Ctrl Pts',(17.2426267152174,-20.4546419398957,
13.4124566518761));
#176983=CARTESIAN_POINT('Ctrl Pts',(17.3232615220208,-20.5331049076727,
13.4055489324444));
#176984=CARTESIAN_POINT('Ctrl Pts',(17.3929622163251,-20.5926369670539,
13.3997422843461));
#176985=CARTESIAN_POINT('Ctrl Pts',(17.5419203156103,-20.7040139376681,
13.3876785442398));
#176986=CARTESIAN_POINT('Ctrl Pts',(17.621246564242,-20.7554369640963,13.3814262533153));
#176987=CARTESIAN_POINT('Ctrl Pts',(17.7685849134921,-20.8375167217566,
13.3702890295538));
#176988=CARTESIAN_POINT('Ctrl Pts',(17.8352936133738,-20.8702094983373,
13.3654068945094));
#176989=CARTESIAN_POINT('Ctrl Pts',(17.942446797182,-20.9159036065538,13.3579381862308));
#176990=CARTESIAN_POINT('Ctrl Pts',(17.9817988017128,-20.9313099197741,
13.3552710728721));
#176991=CARTESIAN_POINT('Ctrl Pts',(18.0286043447873,-20.9480364423398,
13.3522081873186));
#176992=CARTESIAN_POINT('Ctrl Pts',(18.0356335860942,-20.9505066587893,
13.3517510678581));
#176993=CARTESIAN_POINT('Ctrl Pts',(18.0470291413919,-20.9544438201529,
13.3510147963791));
#176994=CARTESIAN_POINT('Ctrl Pts',(18.0513873874972,-20.9559336904257,
13.350734338428));
#176995=CARTESIAN_POINT('Ctrl Pts',(18.0591363518727,-20.9585544676598,
13.3502377330421));
#176996=CARTESIAN_POINT('Ctrl Pts',(18.0625251018282,-20.9596910213093,
13.3500212553869));
#176997=CARTESIAN_POINT('Ctrl Pts',(18.0698013117486,-20.9621109076413,
13.3495579432307));
#176998=CARTESIAN_POINT('Ctrl Pts',(18.0736896093324,-20.9633915449565,
13.3493112681663));
#176999=CARTESIAN_POINT('Ctrl Pts',(18.0843955200033,-20.9668832192623,
13.3486345247886));
#177000=CARTESIAN_POINT('Ctrl Pts',(18.091220757459,-20.9690709497682,13.3482058072698));
#177001=CARTESIAN_POINT('Ctrl Pts',(18.128070493577,-20.9806765608811,13.3459051235433));
#177002=CARTESIAN_POINT('Ctrl Pts',(18.1582927502702,-20.989459338613,13.3440681189388));
#177003=CARTESIAN_POINT('Ctrl Pts',(18.3467774910431,-21.0397048434727,
13.3328547473846));
#177004=CARTESIAN_POINT('Ctrl Pts',(18.50922207078,-21.0633834123684,13.3242094102949));
#177005=CARTESIAN_POINT('Ctrl Pts',(18.789860587336,-21.0715013976389,13.3088409155415));
#177006=CARTESIAN_POINT('Ctrl Pts',(18.9069971518886,-21.0651666466656,
13.3023034532464));
#177007=CARTESIAN_POINT('Ctrl Pts',(19.0371602860946,-21.047229617872,13.2946060361465));
#177008=CARTESIAN_POINT('Ctrl Pts',(19.0512998056803,-21.0451350002011,
13.2937643058659));
#177009=CARTESIAN_POINT('Ctrl Pts',(19.0737683343618,-21.0415736358923,
13.2924174366657));
#177010=CARTESIAN_POINT('Ctrl Pts',(19.08211179143,-21.0401998655191,13.2919152409463));
#177011=CARTESIAN_POINT('Ctrl Pts',(19.0968115305041,-21.0376889716212,
13.291026752646));
#177012=CARTESIAN_POINT('Ctrl Pts',(19.1031712953016,-21.0365726771472,
13.2906411264571));
#177013=CARTESIAN_POINT('Ctrl Pts',(19.1163141430224,-21.0342037543785,
13.2898416265899));
#177014=CARTESIAN_POINT('Ctrl Pts',(19.1230964022442,-21.0329470360179,
13.2894276267389));
#177015=CARTESIAN_POINT('Ctrl Pts',(19.1404886062956,-21.0296363497948,
13.2883622638528));
#177016=CARTESIAN_POINT('Ctrl Pts',(19.151089088065,-21.0275342625146,13.2877093721325));
#177017=CARTESIAN_POINT('Ctrl Pts',(19.1952560362126,-21.0184238881681,
13.2849739345326));
#177018=CARTESIAN_POINT('Ctrl Pts',(19.228664289554,-21.0106820641266,13.282868070604));
#177019=CARTESIAN_POINT('Ctrl Pts',(19.3152007715219,-20.9884006435209,
13.2773137920213));
#177020=CARTESIAN_POINT('Ctrl Pts',(19.367973078019,-20.9725937826712,13.2738269953561));
#177021=CARTESIAN_POINT('Ctrl Pts',(19.5235313261517,-20.9193054228759,
13.2632580143686));
#177022=CARTESIAN_POINT('Ctrl Pts',(19.624087621682,-20.8758999196903,13.2560274373616));
#177023=CARTESIAN_POINT('Ctrl Pts',(19.7612320605562,-20.803639422771,13.2457873985614));
#177024=CARTESIAN_POINT('Ctrl Pts',(19.8009335352184,-20.7810509233245,
13.2427764779824));
#177025=CARTESIAN_POINT('Ctrl Pts',(19.8593554864681,-20.7452612691464,
13.2383012432287));
#177026=CARTESIAN_POINT('Ctrl Pts',(19.878642827034,-20.7330120160716,13.2368162757804));
#177027=CARTESIAN_POINT('Ctrl Pts',(19.8983116101496,-20.7200689923224,
13.2352967385645));
#177028=CARTESIAN_POINT('Ctrl Pts',(19.8988944629857,-20.7196850333835,
13.235251704772));
#177029=CARTESIAN_POINT('Ctrl Pts',(19.9087866268641,-20.7131614745064,
13.2344873130667));
#177030=CARTESIAN_POINT('Ctrl Pts',(19.9180476216383,-20.7069486019535,
13.2337704997697));
#177031=CARTESIAN_POINT('Ctrl Pts',(19.9605358812947,-20.6779552993115,
13.2304777645199));
#177032=CARTESIAN_POINT('Ctrl Pts',(19.9931601425782,-20.6543008498862,
13.2279377298348));
#177033=CARTESIAN_POINT('Ctrl Pts',(20.0309128500806,-20.6252483415888,
13.2250028957476));
#177034=CARTESIAN_POINT('Ctrl Pts',(20.0367107579682,-20.6207383371908,
13.2245523082544));
#177035=CARTESIAN_POINT('Ctrl Pts',(20.0460809079982,-20.6133710040433,
13.2238244799372));
#177036=CARTESIAN_POINT('Ctrl Pts',(20.0496675121696,-20.6105321584274,
13.2235459804113));
#177037=CARTESIAN_POINT('Ctrl Pts',(20.0560378923598,-20.6054562480978,
13.2230515261108));
#177038=CARTESIAN_POINT('Ctrl Pts',(20.0588252303296,-20.6032237470864,
13.2228352519729));
#177039=CARTESIAN_POINT('Ctrl Pts',(20.064811867015,-20.5984038702072,13.2223709036732));
#177040=CARTESIAN_POINT('Ctrl Pts',(20.0680092664162,-20.5958142252089,
13.2221229966954));
#177041=CARTESIAN_POINT('Ctrl Pts',(20.0768287578111,-20.5886284424818,
13.2214393902693));
#177042=CARTESIAN_POINT('Ctrl Pts',(20.0824348441028,-20.5840126244084,
13.2210050874525));
#177043=CARTESIAN_POINT('Ctrl Pts',(20.1132555913394,-20.558368872483,13.218617978693));
#177044=CARTESIAN_POINT('Ctrl Pts',(20.138003692881,-20.5367841619103,13.2167033145511));
#177045=CARTESIAN_POINT('Ctrl Pts',(20.2821385480707,-20.4050452490167,
13.2054953232617));
#177046=CARTESIAN_POINT('Ctrl Pts',(20.3890376791219,-20.282013335719,13.1969092747812));
#177047=CARTESIAN_POINT('Ctrl Pts',(20.5467790335773,-20.0516148386093,
13.1816227856056));
#177048=CARTESIAN_POINT('Ctrl Pts',(20.6046458040868,-19.9499978158022,
13.1751046545738));
#177049=CARTESIAN_POINT('Ctrl Pts',(20.659860107084,-19.8311791747816,13.1674289980549));
#177050=CARTESIAN_POINT('Ctrl Pts',(20.6657502254931,-19.8181606229958,
13.1665875466499));
#177051=CARTESIAN_POINT('Ctrl Pts',(20.6749148631388,-19.7973460660373,
13.1652410403313));
#177052=CARTESIAN_POINT('Ctrl Pts',(20.6782753076995,-19.7895882055193,
13.1647389261077));
#177053=CARTESIAN_POINT('Ctrl Pts',(20.6841200519565,-19.7758704224686,
13.1638505327387));
#177054=CARTESIAN_POINT('Ctrl Pts',(20.6866237373739,-19.7699188400323,
13.1634649195282));
#177055=CARTESIAN_POINT('Ctrl Pts',(20.6917459140025,-19.7575852051199,
13.1626653981998));
#177056=CARTESIAN_POINT('Ctrl Pts',(20.6943605132158,-19.7512016284852,
13.162251363671));
#177057=CARTESIAN_POINT('Ctrl Pts',(20.7009919329376,-19.7347825882444,
13.161185809666));
#177058=CARTESIAN_POINT('Ctrl Pts',(20.7049631388679,-19.7247290230976,
13.1605327604457));
#177059=CARTESIAN_POINT('Ctrl Pts',(20.7212181732176,-19.6826369044582,
13.1577957965077));
#177060=CARTESIAN_POINT('Ctrl Pts',(20.7327985895077,-19.6503339718685,
13.1556885311821));
#177061=CARTESIAN_POINT('Ctrl Pts',(20.7609232956757,-19.5654405682352,
13.150129674959));
#177062=CARTESIAN_POINT('Ctrl Pts',(20.7762066870715,-19.5124626686873,
13.146639623127));
#177063=CARTESIAN_POINT('Ctrl Pts',(20.8156045875079,-19.3527264517247,
13.1360643892891));
#177064=CARTESIAN_POINT('Ctrl Pts',(20.8335284396875,-19.244636657503,13.1288308354333));
#177065=CARTESIAN_POINT('Ctrl Pts',(20.8473035808731,-19.0864493140128,
13.1183419000024));
#177066=CARTESIAN_POINT('Ctrl Pts',(20.8498652528019,-19.0371065782503,
13.1150857622981));
#177067=CARTESIAN_POINT('Ctrl Pts',(20.8509809436253,-18.9709897139606,
13.1107737986976));
#177068=CARTESIAN_POINT('Ctrl Pts',(20.8510649132769,-18.9542580605904,
13.1096870245731));
#177069=CARTESIAN_POINT('Ctrl Pts',(20.8505861283816,-18.884227330431,13.1051610039506));
#177070=CARTESIAN_POINT('Ctrl Pts',(20.848208890954,-18.8309554902276,13.1017727801264));
#177071=CARTESIAN_POINT('Ctrl Pts',(20.8431056135174,-18.7691380252512,
13.0979464593096));
#177072=CARTESIAN_POINT('Ctrl Pts',(20.8423347399558,-18.7604546500727,
13.0974114224516));
#177073=CARTESIAN_POINT('Ctrl Pts',(20.841086278737,-18.7473136364838,13.0966056703895));
#177074=CARTESIAN_POINT('Ctrl Pts',(20.8406481444158,-18.7428524684915,
13.0963328199396));
#177075=CARTESIAN_POINT('Ctrl Pts',(20.8398362409872,-18.7348469955922,
13.0958444751359));
#177076=CARTESIAN_POINT('Ctrl Pts',(20.8394676904449,-18.731302228704,13.0956286928499));
#177077=CARTESIAN_POINT('Ctrl Pts',(20.8386473941704,-18.7236016189139,
13.0951609195154));
#177078=CARTESIAN_POINT('Ctrl Pts',(20.8381922918668,-18.7194461915745,
13.0949091196381));
#177079=CARTESIAN_POINT('Ctrl Pts',(20.8368793044891,-18.7077771083128,
13.0942037046564));
#177080=CARTESIAN_POINT('Ctrl Pts',(20.8359934530151,-18.7002665745964,
13.0937516363689));
#177081=CARTESIAN_POINT('Ctrl Pts',(20.830455660632,-18.6553841811548,13.0910609516067));
#177082=CARTESIAN_POINT('Ctrl Pts',(20.824847096688,-18.6181346172033,13.0888728180889));
#177083=CARTESIAN_POINT('Ctrl Pts',(20.8031134411284,-18.496019612851,13.0817900122105));
#177084=CARTESIAN_POINT('Ctrl Pts',(20.7827888462894,-18.4119859557136,
13.0770590790458));
#177085=CARTESIAN_POINT('Ctrl Pts',(20.7055121139417,-18.1608351397468,
13.062759428103));
#177086=CARTESIAN_POINT('Ctrl Pts',(20.6327808707394,-17.9994106869022,
13.0532808826202));
#177087=CARTESIAN_POINT('Ctrl Pts',(20.5289324871061,-17.8293103912452,
13.0416993708831));
#177088=CARTESIAN_POINT('Ctrl Pts',(20.5166696699022,-17.8099389777776,
13.0403561933104));
#177089=CARTESIAN_POINT('Ctrl Pts',(20.4988645988361,-17.7827981902561,
13.0384378849605));
#177090=CARTESIAN_POINT('Ctrl Pts',(20.4935804376063,-17.7748608394905,
13.0378723803512));
#177091=CARTESIAN_POINT('Ctrl Pts',(20.4849038996384,-17.76201675878,13.0369498357122));
#177092=CARTESIAN_POINT('Ctrl Pts',(20.4815440523285,-17.7570881353827,
13.03659402749));
#177093=CARTESIAN_POINT('Ctrl Pts',(20.4744645819832,-17.7467968502279,
13.0358472574289));
#177094=CARTESIAN_POINT('Ctrl Pts',(20.4707409054794,-17.7414370651996,
13.03545614369));
#177095=CARTESIAN_POINT('Ctrl Pts',(20.4618179253979,-17.7287194160525,
13.0345228379104));
#177096=CARTESIAN_POINT('Ctrl Pts',(20.4565963498529,-17.7213774006869,
13.0339797951546));
#177097=CARTESIAN_POINT('Ctrl Pts',(20.4388204472616,-17.6967176593755,
13.0321413620442));
#177098=CARTESIAN_POINT('Ctrl Pts',(20.4260508916097,-17.6795573727676,
13.0308376660798));
#177099=CARTESIAN_POINT('Ctrl Pts',(20.3549308423918,-17.5869470855236,
13.0236651602311));
#177100=CARTESIAN_POINT('Ctrl Pts',(20.2917998392333,-17.5153226987362,
13.0176067238052));
#177101=CARTESIAN_POINT('Ctrl Pts',(20.1028893331245,-17.3281371873796,
13.000324262642));
#177102=CARTESIAN_POINT('Ctrl Pts',(19.9676555988288,-17.2231624718423,
12.9888143036815));
#177103=CARTESIAN_POINT('Ctrl Pts',(19.7898606076211,-17.1167371733214,
12.9755907225459));
#177104=CARTESIAN_POINT('Ctrl Pts',(19.7579396454261,-17.0987382157179,
12.9732863797859));
#177105=CARTESIAN_POINT('Ctrl Pts',(19.7192637075255,-17.0782349935799,
12.9705907868171));
#177106=CARTESIAN_POINT('Ctrl Pts',(19.7129450074818,-17.0749260674434,
12.9701534098925));
#177107=CARTESIAN_POINT('Ctrl Pts',(19.7026042291792,-17.069577310355,12.9694426877544));
#177108=CARTESIAN_POINT('Ctrl Pts',(19.6985922028414,-17.0675183157266,
12.9691681770724));
#177109=CARTESIAN_POINT('Ctrl Pts',(19.6913960297823,-17.0638542014124,
12.96867805248));
#177110=CARTESIAN_POINT('Ctrl Pts',(19.6882143907067,-17.0622442983973,
12.9684621413788));
#177111=CARTESIAN_POINT('Ctrl Pts',(19.681312048549,-17.0587736035999,12.9679954465931));
#177112=CARTESIAN_POINT('Ctrl Pts',(19.6775899356073,-17.0569157434413,
12.9677448467576));
#177113=CARTESIAN_POINT('Ctrl Pts',(19.6671694597689,-17.051752766001,12.9670461758156));
#177114=CARTESIAN_POINT('Ctrl Pts',(19.660458969413,-17.0484720719851,12.9665996043409));
#177115=CARTESIAN_POINT('Ctrl Pts',(19.6212336124819,-17.0295517387198,
12.9640079149118));
#177116=CARTESIAN_POINT('Ctrl Pts',(19.5883384451109,-17.0147088572662,
12.9619090544536));
#177117=CARTESIAN_POINT('Ctrl Pts',(19.4810317920743,-16.9695555214973,
12.955250124887));
#177118=CARTESIAN_POINT('Ctrl Pts',(19.4052662102834,-16.9426353487972,
12.9508321908856));
#177119=CARTESIAN_POINT('Ctrl Pts',(19.1503059658817,-16.8680828694102,
12.9363521853746));
#177120=CARTESIAN_POINT('Ctrl Pts',(18.9664274996373,-16.8396570639553,
12.9264403975662));
#177121=CARTESIAN_POINT('Ctrl Pts',(18.7590649119399,-16.8350326020103,
12.9143775668019));
#177122=CARTESIAN_POINT('Ctrl Pts',(18.7369239058494,-16.8348862547774,
12.9130796949431));
#177123=CARTESIAN_POINT('Ctrl Pts',(18.706321392983,-16.8351640266937,12.9112706640304));
#177124=CARTESIAN_POINT('Ctrl Pts',(18.6978581448685,-16.8352916104678,
12.9107687689959));
#177125=CARTESIAN_POINT('Ctrl Pts',(18.6833179082467,-16.8355980332273,
12.9099036533708));
#177126=CARTESIAN_POINT('Ctrl Pts',(18.6772404642275,-16.8357523034161,
12.9095412053612));
#177127=CARTESIAN_POINT('Ctrl Pts',(18.6647182574314,-16.8361241477764,
12.9087926119722));
#177128=CARTESIAN_POINT('Ctrl Pts',(18.658273661797,-16.8363449945344,12.9084063678128));
#177129=CARTESIAN_POINT('Ctrl Pts',(18.6432880912628,-16.8369270868709,
12.9075059189655));
#177130=CARTESIAN_POINT('Ctrl Pts',(18.6347481399251,-16.8373106272641,
12.9069910203738));
#177131=CARTESIAN_POINT('Ctrl Pts',(18.6074589418945,-16.8387018884347,
12.905339950942));
#177132=CARTESIAN_POINT('Ctrl Pts',(18.5887210843969,-16.8399073058309,
12.9041976091759));
#177133=CARTESIAN_POINT('Ctrl Pts',(18.4954173678868,-16.8471570580516,
12.8984647549626));
#177134=CARTESIAN_POINT('Ctrl Pts',(18.4212002243108,-16.8569010390327,
12.8937595130517));
#177135=CARTESIAN_POINT('Ctrl Pts',(18.2406583913333,-16.8904115271796,
12.8819630746622));
#177136=CARTESIAN_POINT('Ctrl Pts',(18.1353541948544,-16.9184925143993,
12.8747714025496));
#177137=CARTESIAN_POINT('Ctrl Pts',(17.9193969649913,-16.994315889852,12.8596504024579));
#177138=CARTESIAN_POINT('Ctrl Pts',(17.8096848777122,-17.0436621333496,
12.8517488716262));
#177139=CARTESIAN_POINT('Ctrl Pts',(17.6964353806998,-17.1066710432259,
12.8437444585833));
#177140=CARTESIAN_POINT('Ctrl Pts',(17.688162584794,-17.1113470162397,12.843160736693));
#177141=CARTESIAN_POINT('Ctrl Pts',(17.6759477966824,-17.1183600328319,
12.8423006712227));
#177142=CARTESIAN_POINT('Ctrl Pts',(17.6719815876047,-17.1206543508156,
12.842021686721));
#177143=CARTESIAN_POINT('Ctrl Pts',(17.6650364034486,-17.1247020556958,
12.8415337012998));
#177144=CARTESIAN_POINT('Ctrl Pts',(17.6620542463398,-17.1264498774787,
12.8413243454292));
#177145=CARTESIAN_POINT('Ctrl Pts',(17.6556512776278,-17.1302237132594,
12.8408752306159));
#177146=CARTESIAN_POINT('Ctrl Pts',(17.652231897653,-17.1322520561036,12.8406356262337));
#177147=CARTESIAN_POINT('Ctrl Pts',(17.6451799244936,-17.136462118738,12.8401419234826));
#177148=CARTESIAN_POINT('Ctrl Pts',(17.6415481234872,-17.1386451386098,
12.8398879099939));
#177149=CARTESIAN_POINT('Ctrl Pts',(17.6324202174276,-17.1441691585595,
12.8392500473204));
#177150=CARTESIAN_POINT('Ctrl Pts',(17.6269326955955,-17.1475243546957,
12.838867086624));
#177151=CARTESIAN_POINT('Ctrl Pts',(17.6113368329068,-17.1571579439384,
12.8377798952498));
#177152=CARTESIAN_POINT('Ctrl Pts',(17.6012658514682,-17.1634967276001,
12.8370792964518));
#177153=CARTESIAN_POINT('Ctrl Pts',(17.5675209042162,-17.1851355376233,
12.8347348248868));
#177154=CARTESIAN_POINT('Ctrl Pts',(17.544098305885,-17.2008239329634,12.8331125786159));
#177155=CARTESIAN_POINT('Ctrl Pts',(17.3581666306147,-17.3308141126764,
12.8202170994803));
#177156=CARTESIAN_POINT('Ctrl Pts',(17.2121628972259,-17.4670122003588,
12.8098882853186));
#177157=CARTESIAN_POINT('Ctrl Pts',(17.0417071984194,-17.6779933069495,
12.7947236966457));
#177158=CARTESIAN_POINT('Ctrl Pts',(16.9990658991834,-17.7367016704979,
12.7905873052676));
#177159=CARTESIAN_POINT('Ctrl Pts',(16.9524196872294,-17.8083959362725,
12.7855679569305));
#177160=CARTESIAN_POINT('Ctrl Pts',(16.9454171332413,-17.8193791530976,
12.784799939161));
#177161=CARTESIAN_POINT('Ctrl Pts',(16.9341882116226,-17.8373550918691,
12.7835441029886));
#177162=CARTESIAN_POINT('Ctrl Pts',(16.9299001205676,-17.8443089930049,
12.7830585681133));
#177163=CARTESIAN_POINT('Ctrl Pts',(16.922326592965,-17.8567514516854,12.7821902283659));
#177164=CARTESIAN_POINT('Ctrl Pts',(16.9190255622627,-17.8622304347635,
12.7818080016268));
#177165=CARTESIAN_POINT('Ctrl Pts',(16.9121128752751,-17.8738225015948,
12.7809995722677));
#177166=CARTESIAN_POINT('Ctrl Pts',(16.90850704683,-17.879938952615,12.7805731633502));
#177167=CARTESIAN_POINT('Ctrl Pts',(16.8990295382294,-17.8962018044484,
12.7794397359913));
#177168=CARTESIAN_POINT('Ctrl Pts',(16.8932113128699,-17.9063789281139,
12.7787307951482));
#177169=CARTESIAN_POINT('Ctrl Pts',(16.8663371941056,-17.9543061334403,
12.7753933757275));
#177170=CARTESIAN_POINT('Ctrl Pts',(16.8463573856811,-17.9926448320317,
12.7727268165693));
#177171=CARTESIAN_POINT('Ctrl Pts',(16.7969423861428,-18.0949948546981,
12.7656112185025));
#177172=CARTESIAN_POINT('Ctrl Pts',(16.769532030164,-18.1598529613437,12.7611038352746));
#177173=CARTESIAN_POINT('Ctrl Pts',(16.745419233475,-18.2258901357186,12.7565301047573));
#177174=CARTESIAN_POINT('Ctrl Pts',(16.7454193796745,-18.2258897353253,
12.5316746168857));
#177175=CARTESIAN_POINT('Ctrl Pts',(16.7953825891274,-18.0890567019958,
12.5406319683147));
#177176=CARTESIAN_POINT('Ctrl Pts',(16.8593353085734,-17.9577454254152,
12.550071381493));
#177177=CARTESIAN_POINT('Ctrl Pts',(16.9723432228534,-17.7760228803993,
12.5641884471658));
#177178=CARTESIAN_POINT('Ctrl Pts',(17.0112103367997,-17.719785447589,12.5687174101842));
#177179=CARTESIAN_POINT('Ctrl Pts',(17.0993279127861,-17.6046261183628,
12.5782308960913));
#177180=CARTESIAN_POINT('Ctrl Pts',(17.1492063641352,-17.5462970787643,
12.5831967070055));
#177181=CARTESIAN_POINT('Ctrl Pts',(17.2123286753608,-17.4801226050842,
12.5888934963698));
#177182=CARTESIAN_POINT('Ctrl Pts',(17.2226240058597,-17.4695529290772,
12.5898054030657));
#177183=CARTESIAN_POINT('Ctrl Pts',(17.2360186887604,-17.4560859113639,
12.5909688368337));
#177184=CARTESIAN_POINT('Ctrl Pts',(17.2390171054497,-17.4530893571951,
12.5912278139004));
#177185=CARTESIAN_POINT('Ctrl Pts',(17.2448933532595,-17.4472519325436,
12.5917324727961));
#177186=CARTESIAN_POINT('Ctrl Pts',(17.2477703619008,-17.4444102629199,
12.5919782163282));
#177187=CARTESIAN_POINT('Ctrl Pts',(17.2532122418611,-17.4390659443687,
12.5924404947478));
#177188=CARTESIAN_POINT('Ctrl Pts',(17.2557752935004,-17.4365615952422,
12.5926571602218));
#177189=CARTESIAN_POINT('Ctrl Pts',(17.2616503745035,-17.4308501604457,
12.593151405721));
#177190=CARTESIAN_POINT('Ctrl Pts',(17.2649665253785,-17.4276473815295,
12.593428649504));
#177191=CARTESIAN_POINT('Ctrl Pts',(17.2737994418166,-17.419172037262,12.5941626251894));
#177192=CARTESIAN_POINT('Ctrl Pts',(17.2793343563971,-17.4139183692787,
12.5946179310359));
#177193=CARTESIAN_POINT('Ctrl Pts',(17.3183293418311,-17.3773036286071,
12.5977944975953));
#177194=CARTESIAN_POINT('Ctrl Pts',(17.3527749539149,-17.3470046349497,
12.6004406740512));
#177195=CARTESIAN_POINT('Ctrl Pts',(17.3951824644032,-17.3120796083725,
12.603550664452));
#177196=CARTESIAN_POINT('Ctrl Pts',(17.4022216829578,-17.306357936064,12.6040621917369));
#177197=CARTESIAN_POINT('Ctrl Pts',(17.4099491733159,-17.3001588737882,
12.6046188905966));
#177198=CARTESIAN_POINT('Ctrl Pts',(17.4106011157436,-17.299636513645,12.6046658199872));
#177199=CARTESIAN_POINT('Ctrl Pts',(17.4342094165713,-17.2807436132308,
12.6063638915347));
#177200=CARTESIAN_POINT('Ctrl Pts',(17.4575463733341,-17.2628523717006,
12.6079963931372));
#177201=CARTESIAN_POINT('Ctrl Pts',(17.5992509773371,-17.1588291430084,
12.6176857349932));
#177202=CARTESIAN_POINT('Ctrl Pts',(17.7259175469084,-17.084678858069,12.6254645859661));
#177203=CARTESIAN_POINT('Ctrl Pts',(17.9082090157549,-17.0019610463819,
12.63660735487));
#177204=CARTESIAN_POINT('Ctrl Pts',(17.9580210497439,-16.9816094974997,
12.6396435760365));
#177205=CARTESIAN_POINT('Ctrl Pts',(18.0400903766667,-16.9516736579726,
12.6446720630314));
#177206=CARTESIAN_POINT('Ctrl Pts',(18.0718969361652,-16.9409218343537,
12.6466268836571));
#177207=CARTESIAN_POINT('Ctrl Pts',(18.1142608484227,-16.9277151496887,
12.6492439561571));
#177208=CARTESIAN_POINT('Ctrl Pts',(18.1246015714009,-16.9245781593697,
12.6498837963592));
#177209=CARTESIAN_POINT('Ctrl Pts',(18.1415813665529,-16.9195687615708,
12.6509362994865));
#177210=CARTESIAN_POINT('Ctrl Pts',(18.1482064560571,-16.9176493669129,
12.6513474222978));
#177211=CARTESIAN_POINT('Ctrl Pts',(18.1610514975836,-16.9139959010065,
12.6521454698726));
#177212=CARTESIAN_POINT('Ctrl Pts',(18.167270242815,-16.9122578410928,12.6525322595226));
#177213=CARTESIAN_POINT('Ctrl Pts',(18.1816512760415,-16.9083093689384,
12.6534277481885));
#177214=CARTESIAN_POINT('Ctrl Pts',(18.1898190101251,-16.9061193692287,
12.6539371038416));
#177215=CARTESIAN_POINT('Ctrl Pts',(18.2118290376171,-16.9003589883457,
12.6553118353226));
#177216=CARTESIAN_POINT('Ctrl Pts',(18.2256945515284,-16.8968798307697,
12.6561801420232));
#177217=CARTESIAN_POINT('Ctrl Pts',(18.3536111382608,-16.8661564866326,
12.6642129062706));
#177218=CARTESIAN_POINT('Ctrl Pts',(18.4696875071382,-16.8482961546333,
12.6716813753892));
#177219=CARTESIAN_POINT('Ctrl Pts',(18.7501379817577,-16.828725674465,12.6900475499762));
#177220=CARTESIAN_POINT('Ctrl Pts',(18.9144144661925,-16.8363428478961,
12.7010881716108));
#177221=CARTESIAN_POINT('Ctrl Pts',(19.1068481775076,-16.8678599255837,
12.7134620491664));
#177222=CARTESIAN_POINT('Ctrl Pts',(19.1374173068122,-16.8735606030679,
12.7154087152327));
#177223=CARTESIAN_POINT('Ctrl Pts',(19.1748402553571,-16.8813962589408,
12.7177593564414));
#177224=CARTESIAN_POINT('Ctrl Pts',(19.1818216264899,-16.8828949332069,
12.718196475163));
#177225=CARTESIAN_POINT('Ctrl Pts',(19.192787739894,-16.8853071056056,12.7188807371032));
#177226=CARTESIAN_POINT('Ctrl Pts',(19.1967775718533,-16.8861968560242,
12.7191292036989));
#177227=CARTESIAN_POINT('Ctrl Pts',(19.2042521005376,-16.8878864507214,
12.7195937271743));
#177228=CARTESIAN_POINT('Ctrl Pts',(19.207737307959,-16.8886835565927,12.7198099313323));
#177229=CARTESIAN_POINT('Ctrl Pts',(19.2157168800142,-16.8905298579046,
12.7203040603352));
#177230=CARTESIAN_POINT('Ctrl Pts',(19.220209836522,-16.8915849216637,12.7205816446536));
#177231=CARTESIAN_POINT('Ctrl Pts',(19.2319770181782,-16.8943887974403,
12.7213070563906));
#177232=CARTESIAN_POINT('Ctrl Pts',(19.2392455589961,-16.8961615091662,
12.721753545481));
#177233=CARTESIAN_POINT('Ctrl Pts',(19.2880753492403,-16.908345133074,12.724743237497));
#177234=CARTESIAN_POINT('Ctrl Pts',(19.3293247931082,-16.919977938457,12.727220989108));
#177235=CARTESIAN_POINT('Ctrl Pts',(19.378859274571,-16.9355853540229,12.7301693795168));
#177236=CARTESIAN_POINT('Ctrl Pts',(19.3875052723908,-16.9383708455907,
12.730682992802));
#177237=CARTESIAN_POINT('Ctrl Pts',(19.4096844266208,-16.9456742278369,
12.731998550123));
#177238=CARTESIAN_POINT('Ctrl Pts',(19.4231904463482,-16.9502734725934,
12.7327977477369));
#177239=CARTESIAN_POINT('Ctrl Pts',(19.5716091996105,-17.0024951953984,
12.7415692161289));
#177240=CARTESIAN_POINT('Ctrl Pts',(19.7014120515451,-17.0635413834698,
12.749165013767));
#177241=CARTESIAN_POINT('Ctrl Pts',(19.90378413461,-17.1850984508933,12.762165895393));
#177242=CARTESIAN_POINT('Ctrl Pts',(19.9802486721115,-17.2381746423221,
12.7673866940842));
#177243=CARTESIAN_POINT('Ctrl Pts',(20.0694783863763,-17.3092487069926,
12.7740313407989));
#177244=CARTESIAN_POINT('Ctrl Pts',(20.085786893264,-17.3226423109305,12.7752698471986));
#177245=CARTESIAN_POINT('Ctrl Pts',(20.1087310498337,-17.3420671327836,
12.7770483077694));
#177246=CARTESIAN_POINT('Ctrl Pts',(20.1155331567506,-17.3479004303477,
12.7775801716598));
#177247=CARTESIAN_POINT('Ctrl Pts',(20.1272183604053,-17.3580507916412,
12.7785019677106));
#177248=CARTESIAN_POINT('Ctrl Pts',(20.1321189677088,-17.362347575957,12.7788910556131));
#177249=CARTESIAN_POINT('Ctrl Pts',(20.1414741574155,-17.3706267996846,
12.7796386690936));
#177250=CARTESIAN_POINT('Ctrl Pts',(20.1459318802807,-17.3746056083598,
12.7799970403982));
#177251=CARTESIAN_POINT('Ctrl Pts',(20.1575014868815,-17.3850205746061,
12.7809327816542));
#177252=CARTESIAN_POINT('Ctrl Pts',(20.1645865196243,-17.3914862359164,
12.7815113962661));
#177253=CARTESIAN_POINT('Ctrl Pts',(20.1887073463387,-17.4138007485738,
12.7835006946144));
#177254=CARTESIAN_POINT('Ctrl Pts',(20.2055251866275,-17.4298817529812,
12.7849212887889));
#177255=CARTESIAN_POINT('Ctrl Pts',(20.3440312240785,-17.5667606180304,
12.7969105088962));
#177256=CARTESIAN_POINT('Ctrl Pts',(20.4508723801858,-17.7016336550456,
12.8081469295512));
#177257=CARTESIAN_POINT('Ctrl Pts',(20.5871342162755,-17.9245478486149,
12.8254113663581));
#177258=CARTESIAN_POINT('Ctrl Pts',(20.6290758426579,-18.0041319273194,
12.8313410094519));
#177259=CARTESIAN_POINT('Ctrl Pts',(20.6815953770312,-18.121309793168,12.8395443431179));
#177260=CARTESIAN_POINT('Ctrl Pts',(20.6963944633231,-18.1569010284677,
12.8419694631999));
#177261=CARTESIAN_POINT('Ctrl Pts',(20.712944126124,-18.1999846494188,12.844809751787));
#177262=CARTESIAN_POINT('Ctrl Pts',(20.7156353498323,-18.2071051844952,
12.8452760972875));
#177263=CARTESIAN_POINT('Ctrl Pts',(20.7197486797973,-18.2181684492128,
12.8459957315367));
#177264=CARTESIAN_POINT('Ctrl Pts',(20.7211975509218,-18.2221010627762,
12.846250574659));
#177265=CARTESIAN_POINT('Ctrl Pts',(20.7238565808022,-18.229384969042,12.8467207766399));
#177266=CARTESIAN_POINT('Ctrl Pts',(20.7250699473992,-18.2327349862536,
12.8469363208114));
#177267=CARTESIAN_POINT('Ctrl Pts',(20.7277860844522,-18.2402935864786,
12.8474210598012));
#177268=CARTESIAN_POINT('Ctrl Pts',(20.7292839858799,-18.2445038613987,
12.8476899634007));
#177269=CARTESIAN_POINT('Ctrl Pts',(20.7336431879201,-18.2568805874098,
12.8484772923799));
#177270=CARTESIAN_POINT('Ctrl Pts',(20.736467803333,-18.2650599886678,12.8489935927151));
#177271=CARTESIAN_POINT('Ctrl Pts',(20.7558510926441,-18.3223249176739,
12.8525817392031));
#177272=CARTESIAN_POINT('Ctrl Pts',(20.7706547855483,-18.3719907101684,
12.8555580424725));
#177273=CARTESIAN_POINT('Ctrl Pts',(20.7889978036788,-18.4429476385196,
12.859685062801));
#177274=CARTESIAN_POINT('Ctrl Pts',(20.7940565889579,-18.4638226003992,
12.8608841242494));
#177275=CARTESIAN_POINT('Ctrl Pts',(20.8292168204339,-18.6192042241958,
12.8697211025083));
#177276=CARTESIAN_POINT('Ctrl Pts',(20.8464361234239,-18.7562888512858,
12.8770516681324));
#177277=CARTESIAN_POINT('Ctrl Pts',(20.8526909284411,-18.984813333524,12.8896554717419));
#177278=CARTESIAN_POINT('Ctrl Pts',(20.8493361918441,-19.0756043067693,
12.8947578849793));
#177279=CARTESIAN_POINT('Ctrl Pts',(20.8380619449433,-19.1866195387204,
12.9012593001847));
#177280=CARTESIAN_POINT('Ctrl Pts',(20.8356513405907,-19.207312735762,12.9024821747734));
#177281=CARTESIAN_POINT('Ctrl Pts',(20.8317737298706,-19.2368049283457,
12.9042420604276));
#177282=CARTESIAN_POINT('Ctrl Pts',(20.8305558530335,-19.2456358635337,
12.9047712138997));
#177283=CARTESIAN_POINT('Ctrl Pts',(20.8283522580869,-19.260901262554,12.9056898093815));
#177284=CARTESIAN_POINT('Ctrl Pts',(20.8273925647315,-19.2673394035452,
12.9060784231051));
#177285=CARTESIAN_POINT('Ctrl Pts',(20.8254934735185,-19.2796886839866,
12.9068261815068));
#177286=CARTESIAN_POINT('Ctrl Pts',(20.8245586683405,-19.2856004743193,
12.9071851769834));
#177287=CARTESIAN_POINT('Ctrl Pts',(20.8220516913691,-19.3010303711591,
12.9081248975568));
#177288=CARTESIAN_POINT('Ctrl Pts',(20.8204395199626,-19.3105417556434,
12.9087068881774));
#177289=CARTESIAN_POINT('Ctrl Pts',(20.8146595317652,-19.3432823478781,
12.9107198218279));
#177290=CARTESIAN_POINT('Ctrl Pts',(20.8101684461189,-19.3664520183281,
12.9121609943188));
#177291=CARTESIAN_POINT('Ctrl Pts',(20.7711441683131,-19.5511904291212,
12.9237898335411));
#177292=CARTESIAN_POINT('Ctrl Pts',(20.7181975470318,-19.7082578337931,
12.934592027523));
#177293=CARTESIAN_POINT('Ctrl Pts',(20.5930493756557,-19.9727152551533,
12.9539265624109));
#177294=CARTESIAN_POINT('Ctrl Pts',(20.5282543265012,-20.0827441635174,
12.9623538755103));
#177295=CARTESIAN_POINT('Ctrl Pts',(20.4469595063022,-20.1960267228779,
12.9710015840332));
#177296=CARTESIAN_POINT('Ctrl Pts',(20.4398861615423,-20.2057085692402,
12.9717402867579));
#177297=CARTESIAN_POINT('Ctrl Pts',(20.4297252021208,-20.2193714550986,
12.9727815694726));
#177298=CARTESIAN_POINT('Ctrl Pts',(20.4267051993937,-20.2234021690459,
12.9730886146112));
#177299=CARTESIAN_POINT('Ctrl Pts',(20.4214803080055,-20.2303240706963,
12.9736155926085));
#177300=CARTESIAN_POINT('Ctrl Pts',(20.4192823122238,-20.2332204137115,
12.9738360030218));
#177301=CARTESIAN_POINT('Ctrl Pts',(20.4150096323128,-20.2388205898798,
12.9742619717701));
#177302=CARTESIAN_POINT('Ctrl Pts',(20.4129358810608,-20.241525076194,12.9744675953067));
#177303=CARTESIAN_POINT('Ctrl Pts',(20.4073307631139,-20.2487985591644,
12.9750203972164));
#177304=CARTESIAN_POINT('Ctrl Pts',(20.4037871880083,-20.2533581729778,
12.9753667199411));
#177305=CARTESIAN_POINT('Ctrl Pts',(20.3906100423283,-20.2701711246706,
12.9766431629238));
#177306=CARTESIAN_POINT('Ctrl Pts',(20.3808596222771,-20.2823328014786,
12.97756534501));
#177307=CARTESIAN_POINT('Ctrl Pts',(20.2843015346713,-20.4000807595963,
12.9864949130558));
#177308=CARTESIAN_POINT('Ctrl Pts',(20.1875821062503,-20.4971479439714,
12.9938782275807));
#177309=CARTESIAN_POINT('Ctrl Pts',(19.9630237698075,-20.6826265581204,
13.0096948169346));
#177310=CARTESIAN_POINT('Ctrl Pts',(19.8334828563456,-20.7676810568081,
13.0181143258019));
#177311=CARTESIAN_POINT('Ctrl Pts',(19.6768994536994,-20.8475426753486,
13.0283508671624));
#177312=CARTESIAN_POINT('Ctrl Pts',(19.6578075303315,-20.8569202115095,
13.0295990380894));
#177313=CARTESIAN_POINT('Ctrl Pts',(19.6304507546937,-20.8698492774063,
13.031388972863));
#177314=CARTESIAN_POINT('Ctrl Pts',(19.6222991765641,-20.8736384611988,
13.0319225008756));
#177315=CARTESIAN_POINT('Ctrl Pts',(19.6081915342117,-20.8800873182916,
13.0328462652825));
#177316=CARTESIAN_POINT('Ctrl Pts',(19.6022468120971,-20.8827716118845,
13.0332356475825));
#177317=CARTESIAN_POINT('Ctrl Pts',(19.5908383095093,-20.8878596906219,
13.0339831859697));
#177318=CARTESIAN_POINT('Ctrl Pts',(19.5853765738694,-20.8902679274934,
13.0343411847011));
#177319=CARTESIAN_POINT('Ctrl Pts',(19.571142355586,-20.8964724334231,13.0352745403183));
#177320=CARTESIAN_POINT('Ctrl Pts',(19.5623542891255,-20.9002324129473,
13.0358511294002));
#177321=CARTESIAN_POINT('Ctrl Pts',(19.5322726154318,-20.9128625461953,
13.0378261491551));
#177322=CARTESIAN_POINT('Ctrl Pts',(19.5108602236532,-20.921443886093,13.0392342994339));
#177323=CARTESIAN_POINT('Ctrl Pts',(19.326306323835,-20.9919286662724,13.0513951041409));
#177324=CARTESIAN_POINT('Ctrl Pts',(19.1562576504481,-21.0337807682103,
13.0628424167069));
#177325=CARTESIAN_POINT('Ctrl Pts',(18.8959417254216,-21.0646185923452,
13.0801628129264));
#177326=CARTESIAN_POINT('Ctrl Pts',(18.8082757853792,-21.0695144584377,
13.0859453007544));
#177327=CARTESIAN_POINT('Ctrl Pts',(18.6825553954879,-21.0687159529994,
13.0939733663515));
#177328=CARTESIAN_POINT('Ctrl Pts',(18.6445670799573,-21.0674515218346,
13.0963639261331));
#177329=CARTESIAN_POINT('Ctrl Pts',(18.599062751845,-21.0647087879691,13.0991692089537));
#177330=CARTESIAN_POINT('Ctrl Pts',(18.5914970589351,-21.0642119684073,
13.0996336854787));
#177331=CARTESIAN_POINT('Ctrl Pts',(18.5797601616791,-21.0633778870095,
13.1003510619821));
#177332=CARTESIAN_POINT('Ctrl Pts',(18.5755871019513,-21.0630688913225,
13.1006055010932));
#177333=CARTESIAN_POINT('Ctrl Pts',(18.5678619243686,-21.0624738422157,
13.1010753282678));
#177334=CARTESIAN_POINT('Ctrl Pts',(18.5643096431062,-21.0621911955862,
13.1012908992711));
#177335=CARTESIAN_POINT('Ctrl Pts',(18.5562959071147,-21.0615331947977,
13.1017761649565));
#177336=CARTESIAN_POINT('Ctrl Pts',(18.5518349322269,-21.0611526577067,
13.1020455655842));
#177337=CARTESIAN_POINT('Ctrl Pts',(18.5387170283904,-21.0599917246556,
13.1028357017344));
#177338=CARTESIAN_POINT('Ctrl Pts',(18.5300635387784,-21.0591721514543,
13.1033542894156));
#177339=CARTESIAN_POINT('Ctrl Pts',(18.4689434366683,-21.0530034145317,
13.1069999677989));
#177340=CARTESIAN_POINT('Ctrl Pts',(18.4166831321325,-21.0457481518896,
13.1100279928185));
#177341=CARTESIAN_POINT('Ctrl Pts',(18.3491993660454,-21.0337941039218,
13.1138841982832));
#177342=CARTESIAN_POINT('Ctrl Pts',(18.333685702231,-21.0308666863539,13.114766940754));
#177343=CARTESIAN_POINT('Ctrl Pts',(18.2683553846207,-21.0177804538025,
13.1184737002074));
#177344=CARTESIAN_POINT('Ctrl Pts',(18.2188789466605,-21.0060020544148,
13.121255128417));
#177345=CARTESIAN_POINT('Ctrl Pts',(18.0644203201235,-20.9632986698096,
13.1299802777983));
#177346=CARTESIAN_POINT('Ctrl Pts',(17.961387340135,-20.9260131934354,13.1358712571059));
#177347=CARTESIAN_POINT('Ctrl Pts',(17.8114224938407,-20.8581964004676,
13.1450223107367));
#177348=CARTESIAN_POINT('Ctrl Pts',(17.7620546089211,-20.8335035161518,
13.1481336779481));
#177349=CARTESIAN_POINT('Ctrl Pts',(17.6836215165351,-20.7903615710545,
13.1532834946455));
#177350=CARTESIAN_POINT('Ctrl Pts',(17.6539415157725,-20.7730825620969,
13.1552824397751));
#177351=CARTESIAN_POINT('Ctrl Pts',(17.6154867423497,-20.7494242696181,
13.1579451830577));
#177352=CARTESIAN_POINT('Ctrl Pts',(17.606321106399,-20.7436880919717,13.158585405537));
#177353=CARTESIAN_POINT('Ctrl Pts',(17.5913800202427,-20.7341773699217,
13.1596383772904));
#177354=CARTESIAN_POINT('Ctrl Pts',(17.5855782964891,-20.7304443160173,
13.1600495837561));
#177355=CARTESIAN_POINT('Ctrl Pts',(17.5743824819919,-20.7231628661379,
13.1608476792434));
#177356=CARTESIAN_POINT('Ctrl Pts',(17.5689861673104,-20.719618017182,13.1612344325455));
#177357=CARTESIAN_POINT('Ctrl Pts',(17.5565627299609,-20.7113754357007,
13.1621296703234));
#177358=CARTESIAN_POINT('Ctrl Pts',(17.5495473935714,-20.7066602145462,
13.1626388102793));
#177359=CARTESIAN_POINT('Ctrl Pts',(17.5307542287007,-20.6938646963093,
13.1640125822823));
#177360=CARTESIAN_POINT('Ctrl Pts',(17.5190297833328,-20.6857071157826,
13.1648801388415));
#177361=CARTESIAN_POINT('Ctrl Pts',(17.392421918462,-20.5957014657772,13.1743651173633));
#177362=CARTESIAN_POINT('Ctrl Pts',(17.285932606171,-20.5027010451042,13.1834322353885));
#177363=CARTESIAN_POINT('Ctrl Pts',(17.123405389796,-20.3293207814724,13.1990666158707));
#177364=CARTESIAN_POINT('Ctrl Pts',(17.0622207108439,-20.2543754223836,
13.2054947880728));
#177365=CARTESIAN_POINT('Ctrl Pts',(16.9686660544061,-20.1222738788584,
13.2160579265799));
#177366=CARTESIAN_POINT('Ctrl Pts',(16.933439688745,-20.067315691708,13.220252050226));
#177367=CARTESIAN_POINT('Ctrl Pts',(16.8942250341913,-19.9994207203129,
13.2251234910849));
#177368=CARTESIAN_POINT('Ctrl Pts',(16.8877510526217,-19.9879666666764,
13.2259350796216));
#177369=CARTESIAN_POINT('Ctrl Pts',(16.8788540500336,-19.9718773646439,
13.2270600778773));
#177370=CARTESIAN_POINT('Ctrl Pts',(16.8763409370398,-19.9672926384712,
13.2273789625167));
#177371=CARTESIAN_POINT('Ctrl Pts',(16.8720920943022,-19.9594727929224,
13.2279199303812));
#177372=CARTESIAN_POINT('Ctrl Pts',(16.8703477569948,-19.9562423988482,
13.2281425577202));
#177373=CARTESIAN_POINT('Ctrl Pts',(16.867022326837,-19.9500454237551,13.2285679871242));
#177374=CARTESIAN_POINT('Ctrl Pts',(16.8654398913212,-19.9470796051507,
13.2287708772906));
#177375=CARTESIAN_POINT('Ctrl Pts',(16.8612708347571,-19.9392208993858,
13.2293066266323));
#177376=CARTESIAN_POINT('Ctrl Pts',(16.858696304655,-19.9343215778614,13.2296387232001));
#177377=CARTESIAN_POINT('Ctrl Pts',(16.8496512073231,-19.9169436298722,
13.2308101487592));
#177378=CARTESIAN_POINT('Ctrl Pts',(16.8432855781525,-19.9044104052285,
13.2316431328683));
#177379=CARTESIAN_POINT('Ctrl Pts',(16.7641645765918,-19.7447097402592,
13.2421191975049));
#177380=CARTESIAN_POINT('Ctrl Pts',(16.7086313196221,-19.5896038629917,
13.2508474021997));
#177381=CARTESIAN_POINT('Ctrl Pts',(16.6409703150105,-19.2974349413105,
13.2671776847458));
#177382=CARTESIAN_POINT('Ctrl Pts',(16.6231411419796,-19.1626335726882,
13.2746743954839));
#177383=CARTESIAN_POINT('Ctrl Pts',(16.6177334381976,-19.0102153502626,
13.2835989597362));
#177384=CARTESIAN_POINT('Ctrl Pts',(16.6173369766507,-18.9933619238226,
13.2845914612895));
#177385=CARTESIAN_POINT('Ctrl Pts',(16.6170471058777,-18.9683224448112,
13.2860751509792));
#177386=CARTESIAN_POINT('Ctrl Pts',(16.6169998255314,-18.960138584867,13.2865615214586));
#177387=CARTESIAN_POINT('Ctrl Pts',(16.6170001372645,-18.9455564763432,
13.2874307944041));
#177388=CARTESIAN_POINT('Ctrl Pts',(16.6170292805235,-18.9391582980038,
13.2878131140335));
#177389=CARTESIAN_POINT('Ctrl Pts',(16.6171518843235,-18.9256683305771,
13.2886211575997));
#177390=CARTESIAN_POINT('Ctrl Pts',(16.6172519794772,-18.9185766942862,
13.2890470848809));
#177391=CARTESIAN_POINT('Ctrl Pts',(16.6176113756255,-18.8998005224859,
13.2901778747686));
#177392=CARTESIAN_POINT('Ctrl Pts',(16.6179318027047,-18.8881175247336,
13.2908846438824));
#177393=CARTESIAN_POINT('Ctrl Pts',(16.6198779960632,-18.8336263277381,
13.2941962880927));
#177394=CARTESIAN_POINT('Ctrl Pts',(16.6227060715058,-18.7908736445078,
13.2968385317458));
#177395=CARTESIAN_POINT('Ctrl Pts',(16.6340979511695,-18.6730661229858,
13.3042463160918));
#177396=CARTESIAN_POINT('Ctrl Pts',(16.6453836997484,-18.5983437757388,
13.3090901301051));
#177397=CARTESIAN_POINT('Ctrl Pts',(16.6815642400618,-18.4229141733201,
13.3207652578194));
#177398=CARTESIAN_POINT('Ctrl Pts',(16.7099064233513,-18.3231481995358,
13.3276519349119));
#177399=CARTESIAN_POINT('Ctrl Pts',(16.7454194046024,-18.225889667056,13.3344632333882));
#177400=CARTESIAN_POINT('Origin',(18.734,-18.952,0.));
#177401=CARTESIAN_POINT('',(16.743090036011,-18.2250592052755,14.3554399658108));
#177402=CARTESIAN_POINT('',(16.7454193947488,-18.2258896940418,14.1348940370926));
#177403=CARTESIAN_POINT('',(16.7454193692319,-18.2258897639242,0.));
#177404=CARTESIAN_POINT('',(16.6201365817634,-18.9515404579278,14.311091773925));
#177405=CARTESIAN_POINT('Ctrl Pts',(16.6203928623232,-18.9515314192714,
14.3109441064964));
#177406=CARTESIAN_POINT('Ctrl Pts',(16.6199115702051,-18.7039933214138,
14.3257760596012));
#177407=CARTESIAN_POINT('Ctrl Pts',(16.6606018499745,-18.4566059525848,
14.340608012706));
#177408=CARTESIAN_POINT('Ctrl Pts',(16.743090036011,-18.2250592052755,14.3554399658108));
#177409=CARTESIAN_POINT('Ctrl Pts',(16.6170000287542,-18.9516510797598,
14.3128990382682));
#177410=CARTESIAN_POINT('Ctrl Pts',(16.6169985638884,-18.9605388440599,
14.3123784727587));
#177411=CARTESIAN_POINT('Ctrl Pts',(16.6170530690528,-18.9694264496665,
14.311856218884));
#177412=CARTESIAN_POINT('Ctrl Pts',(16.617270741535,-18.9869375859922,14.3108237482288));
#177413=CARTESIAN_POINT('Ctrl Pts',(16.6174306466636,-18.9955609659129,
14.3103136432639));
#177414=CARTESIAN_POINT('Ctrl Pts',(16.6177963852562,-19.0103940122229,
14.3094332540418));
#177415=CARTESIAN_POINT('Ctrl Pts',(16.6179768689464,-19.0166042359689,
14.3090637645325));
#177416=CARTESIAN_POINT('Ctrl Pts',(16.6183911392992,-19.028982091129,14.3083255017697));
#177417=CARTESIAN_POINT('Ctrl Pts',(16.6186245665712,-19.0351496736629,
14.3079567433572));
#177418=CARTESIAN_POINT('Ctrl Pts',(16.6191442765092,-19.0474570442302,
14.3072190573059));
#177419=CARTESIAN_POINT('Ctrl Pts',(16.619430334278,-19.0535967816614,14.3068501402674));
#177420=CARTESIAN_POINT('Ctrl Pts',(16.6202771218832,-19.0702146333442,
14.3058491214672));
#177421=CARTESIAN_POINT('Ctrl Pts',(16.6208890190741,-19.0806898639952,
14.3052154202335));
#177422=CARTESIAN_POINT('Ctrl Pts',(16.6234852743548,-19.1201005142573,
14.3028208550529));
#177423=CARTESIAN_POINT('Ctrl Pts',(16.6259862441654,-19.1489976250017,
14.301043887867));
#177424=CARTESIAN_POINT('Ctrl Pts',(16.6533334749466,-19.4038925864202,
14.2851745675177));
#177425=CARTESIAN_POINT('Ctrl Pts',(16.7138477085442,-19.6245466791475,
14.2698452627864));
#177426=CARTESIAN_POINT('Ctrl Pts',(16.8322264942422,-19.883816958295,14.2513238062692));
#177427=CARTESIAN_POINT('Ctrl Pts',(16.8583594908963,-19.9353611754857,
14.247627510522));
#177428=CARTESIAN_POINT('Ctrl Pts',(16.8925972239178,-19.9965463788508,
14.2432767012153));
#177429=CARTESIAN_POINT('Ctrl Pts',(16.898718247857,-20.0072640561445,14.2425160201536));
#177430=CARTESIAN_POINT('Ctrl Pts',(16.9074985434946,-20.0223305075977,
14.241449398554));
#177431=CARTESIAN_POINT('Ctrl Pts',(16.9100801887588,-20.0267239131598,
14.2411386985434));
#177432=CARTESIAN_POINT('Ctrl Pts',(16.9145364058199,-20.0342451320219,
14.240607423729));
#177433=CARTESIAN_POINT('Ctrl Pts',(16.9164032337857,-20.0373774885019,
14.2403863509249));
#177434=CARTESIAN_POINT('Ctrl Pts',(16.9200225191191,-20.0434147736011,
14.2399606386637));
#177435=CARTESIAN_POINT('Ctrl Pts',(16.9217738674845,-20.0463203160777,
14.2397559267035));
#177436=CARTESIAN_POINT('Ctrl Pts',(16.9264840170099,-20.0540922862543,
14.23920876601));
#177437=CARTESIAN_POINT('Ctrl Pts',(16.9294555087507,-20.0589510454379,
14.2388671417719));
#177438=CARTESIAN_POINT('Ctrl Pts',(16.9403589057916,-20.0766188727872,
14.2376262872196));
#177439=CARTESIAN_POINT('Ctrl Pts',(16.9484080925125,-20.0893555084984,
14.2367344332985));
#177440=CARTESIAN_POINT('Ctrl Pts',(17.0411047119212,-20.2326240690977,
14.2267199622498));
#177441=CARTESIAN_POINT('Ctrl Pts',(17.1397702716753,-20.3535485650571,
14.2184099905279));
#177442=CARTESIAN_POINT('Ctrl Pts',(17.3441964430362,-20.5542679786293,
14.2028291012479));
#177443=CARTESIAN_POINT('Ctrl Pts',(17.4458690459048,-20.6370903846123,
14.1956355622444));
#177444=CARTESIAN_POINT('Ctrl Pts',(17.5686601993454,-20.7194732505057,
14.1870579580777));
#177445=CARTESIAN_POINT('Ctrl Pts',(17.5829040050208,-20.7287826339327,
14.1860649062725));
#177446=CARTESIAN_POINT('Ctrl Pts',(17.6055868815264,-20.7432203393623,
14.1844857174748));
#177447=CARTESIAN_POINT('Ctrl Pts',(17.6139524436912,-20.7484631743405,
14.1839037753907));
#177448=CARTESIAN_POINT('Ctrl Pts',(17.6282465562387,-20.7572828749356,
14.1829100644459));
#177449=CARTESIAN_POINT('Ctrl Pts',(17.6341565905712,-20.7608895516117,
14.1824993912247));
#177450=CARTESIAN_POINT('Ctrl Pts',(17.6458238516216,-20.7679313353851,
14.1816889728369));
#177451=CARTESIAN_POINT('Ctrl Pts',(17.6515799165101,-20.7713682161675,
14.1812892985924));
#177452=CARTESIAN_POINT('Ctrl Pts',(17.662760227534,-20.7779720153797,14.1805132297018));
#177453=CARTESIAN_POINT('Ctrl Pts',(17.668182439662,-20.7811422519363,14.1801369611862));
#177454=CARTESIAN_POINT('Ctrl Pts',(17.6809398095863,-20.7885251934992,
14.1792518907075));
#177455=CARTESIAN_POINT('Ctrl Pts',(17.6882862277516,-20.7927181354778,
14.1787423810995));
#177456=CARTESIAN_POINT('Ctrl Pts',(17.7081227339754,-20.8038826740534,
14.1773669647971));
#177457=CARTESIAN_POINT('Ctrl Pts',(17.7206585101674,-20.8107718021923,
14.1764981226869));
#177458=CARTESIAN_POINT('Ctrl Pts',(17.8364812946338,-20.8729031838007,
14.1684725470742));
#177459=CARTESIAN_POINT('Ctrl Pts',(17.9440997805178,-20.9196022592869,
14.1610125097963));
#177460=CARTESIAN_POINT('Ctrl Pts',(18.2100568997786,-21.0096608125125,
14.1426693604763));
#177461=CARTESIAN_POINT('Ctrl Pts',(18.3706639288621,-21.0440017959744,
14.1316435710508));
#177462=CARTESIAN_POINT('Ctrl Pts',(18.5648597694148,-21.0624656260514,
14.1192615733656));
#177463=CARTESIAN_POINT('Ctrl Pts',(18.5961610074516,-21.0647409286526,
14.1172965025599));
#177464=CARTESIAN_POINT('Ctrl Pts',(18.6346548631846,-21.0666798389272,
14.1149268088956));
#177465=CARTESIAN_POINT('Ctrl Pts',(18.6418085189274,-21.0670037852376,
14.1144884162702));
#177466=CARTESIAN_POINT('Ctrl Pts',(18.6530528192028,-21.0674558140129,
14.113802609786));
#177467=CARTESIAN_POINT('Ctrl Pts',(18.657142349113,-21.0676083402359,14.1135538628078));
#177468=CARTESIAN_POINT('Ctrl Pts',(18.664804734509,-21.0678718752243,14.1130891013304));
#177469=CARTESIAN_POINT('Ctrl Pts',(18.6683773879172,-21.0679856923264,
14.1128729378517));
#177470=CARTESIAN_POINT('Ctrl Pts',(18.6765563907379,-21.0682255232384,
14.1123792749819));
#177471=CARTESIAN_POINT('Ctrl Pts',(18.6811628664646,-21.0683455463821,
14.112102113721));
#177472=CARTESIAN_POINT('Ctrl Pts',(18.6954029530342,-21.0686700533648,
14.1112479187135));
#177473=CARTESIAN_POINT('Ctrl Pts',(18.7050377512107,-21.0688238100798,
14.1106736490053));
#177474=CARTESIAN_POINT('Ctrl Pts',(18.8024979972458,-21.0697135819577,
14.1048988257154));
#177475=CARTESIAN_POINT('Ctrl Pts',(18.8902987135775,-21.0650492912422,
14.0999755013231));
#177476=CARTESIAN_POINT('Ctrl Pts',(19.0081025781511,-21.0514051105892,
14.093453033427));
#177477=CARTESIAN_POINT('Ctrl Pts',(19.0385597936453,-21.0472034346202,
14.0917744866438));
#177478=CARTESIAN_POINT('Ctrl Pts',(19.176770223872,-21.0250593019557,14.084154294581));
#177479=CARTESIAN_POINT('Ctrl Pts',(19.2831250144684,-20.9994572429335,
14.0782720326108));
#177480=CARTESIAN_POINT('Ctrl Pts',(19.4393112133755,-20.948809056898,14.0691412443895));
#177481=CARTESIAN_POINT('Ctrl Pts',(19.4909139121867,-20.9298248167773,
14.0660414920822));
#177482=CARTESIAN_POINT('Ctrl Pts',(19.5733692925994,-20.8957903053402,
14.0609091886858));
#177483=CARTESIAN_POINT('Ctrl Pts',(19.6046985292448,-20.881959957136,14.0589157905539));
#177484=CARTESIAN_POINT('Ctrl Pts',(19.6454500505661,-20.8627758833888,
14.0562593901813));
#177485=CARTESIAN_POINT('Ctrl Pts',(19.6551872702009,-20.8581006473667,
14.0556198205059));
#177486=CARTESIAN_POINT('Ctrl Pts',(19.6710821685015,-20.8503186170072,
14.0545676489534));
#177487=CARTESIAN_POINT('Ctrl Pts',(19.6772612733218,-20.8472558483541,
14.0541565852843));
#177488=CARTESIAN_POINT('Ctrl Pts',(19.689196921702,-20.8412669319171,14.0533585713872));
#177489=CARTESIAN_POINT('Ctrl Pts',(19.6949552655867,-20.8383445272199,
14.0529717558436));
#177490=CARTESIAN_POINT('Ctrl Pts',(19.7082254701403,-20.8315332623007,
14.0520760889686));
#177491=CARTESIAN_POINT('Ctrl Pts',(19.7157275358983,-20.8276256536899,
14.0515665801786));
#177492=CARTESIAN_POINT('Ctrl Pts',(19.7358522184387,-20.8169894730245,
14.0501911675157));
#177493=CARTESIAN_POINT('Ctrl Pts',(19.7484302227906,-20.8101778465497,
14.0493223282512));
#177494=CARTESIAN_POINT('Ctrl Pts',(19.863127843729,-20.746551637817,14.0413133525316));
#177495=CARTESIAN_POINT('Ctrl Pts',(19.960431704408,-20.6815093911962,14.033871391778));
#177496=CARTESIAN_POINT('Ctrl Pts',(20.1792926898503,-20.5074199805855,
14.0156042039348));
#177497=CARTESIAN_POINT('Ctrl Pts',(20.2946012664589,-20.3916965138818,
14.0046385635982));
#177498=CARTESIAN_POINT('Ctrl Pts',(20.41557440637,-20.2384856072234,13.9922357529867));
#177499=CARTESIAN_POINT('Ctrl Pts',(20.4350579953202,-20.2126108297202,
13.9902062646671));
#177500=CARTESIAN_POINT('Ctrl Pts',(20.4581574237856,-20.1804227558167,
13.9877700342318));
#177501=CARTESIAN_POINT('Ctrl Pts',(20.4623434011426,-20.1745262288418,
13.9873272876515));
#177502=CARTESIAN_POINT('Ctrl Pts',(20.4688598443581,-20.165246551393,13.9866362040669));
#177503=CARTESIAN_POINT('Ctrl Pts',(20.4712107701972,-20.1618779337631,
13.9863865004224));
#177504=CARTESIAN_POINT('Ctrl Pts',(20.4755877109546,-20.1555672001771,
13.9859209181685));
#177505=CARTESIAN_POINT('Ctrl Pts',(20.4776160619388,-20.152626831729,13.9857048847962));
#177506=CARTESIAN_POINT('Ctrl Pts',(20.4822304714435,-20.1459012661219,
13.9852127724995));
#177507=CARTESIAN_POINT('Ctrl Pts',(20.4848116788647,-20.1421128016237,
13.984937023702));
#177508=CARTESIAN_POINT('Ctrl Pts',(20.4927119270671,-20.1304361973155,
13.9840914906566));
#177509=CARTESIAN_POINT('Ctrl Pts',(20.4979902005319,-20.1225204370791,
13.9835243900639));
#177510=CARTESIAN_POINT('Ctrl Pts',(20.5690653040157,-20.0143572906987,
13.9758540865189));
#177511=CARTESIAN_POINT('Ctrl Pts',(20.6262923367506,-19.9087161394295,
13.969271279574));
#177512=CARTESIAN_POINT('Ctrl Pts',(20.7178059936496,-19.6990270984464,
13.9568186765284));
#177513=CARTESIAN_POINT('Ctrl Pts',(20.7535835234111,-19.5960630069706,
13.9509553974396));
#177514=CARTESIAN_POINT('Ctrl Pts',(20.8003489699177,-19.418370751754,13.9407335518356));
#177515=CARTESIAN_POINT('Ctrl Pts',(20.8155537457217,-19.3449784356359,
13.9364855352));
#177516=CARTESIAN_POINT('Ctrl Pts',(20.8296676775589,-19.2523648181068,
13.9310153591968));
#177517=CARTESIAN_POINT('Ctrl Pts',(20.8322509242903,-19.2337535514502,
13.929910790735));
#177518=CARTESIAN_POINT('Ctrl Pts',(20.8356487967478,-19.2066261073567,
13.9282921535242));
#177519=CARTESIAN_POINT('Ctrl Pts',(20.8366601253209,-19.1981351529786,
13.9277842905433));
#177520=CARTESIAN_POINT('Ctrl Pts',(20.8383438635375,-19.183230384364,13.92689056471));
#177521=CARTESIAN_POINT('Ctrl Pts',(20.8390384638506,-19.1768191516539,
13.9265054066274));
#177522=CARTESIAN_POINT('Ctrl Pts',(20.8403308773127,-19.1643586258857,
13.9257553879369));
#177523=CARTESIAN_POINT('Ctrl Pts',(20.8409319507925,-19.1583097289032,
13.925390634115));
#177524=CARTESIAN_POINT('Ctrl Pts',(20.8423073805125,-19.1438347902302,
13.9245161659618));
#177525=CARTESIAN_POINT('Ctrl Pts',(20.8430572825163,-19.1354065791591,
13.924005686868));
#177526=CARTESIAN_POINT('Ctrl Pts',(20.8455851797949,-19.1049263812782,
13.9221547074298));
#177527=CARTESIAN_POINT('Ctrl Pts',(20.8470679493491,-19.0828519497904,
13.9208049852415));
#177528=CARTESIAN_POINT('Ctrl Pts',(20.8577336076008,-18.8755184134431,
13.9080373215584));
#177529=CARTESIAN_POINT('Ctrl Pts',(20.8428740606282,-18.689861664509,13.8958211252233));
#177530=CARTESIAN_POINT('Ctrl Pts',(20.7872334898909,-18.4301219667557,
13.8782833409733));
#177531=CARTESIAN_POINT('Ctrl Pts',(20.7659837045713,-18.3526934096555,
13.8730123855918));
#177532=CARTESIAN_POINT('Ctrl Pts',(20.7288885747899,-18.2424873828691,
13.8655997390942));
#177533=CARTESIAN_POINT('Ctrl Pts',(20.7165166755242,-18.20861815348,13.8633348077176));
#177534=CARTESIAN_POINT('Ctrl Pts',(20.7005444269591,-18.1681328046278,
13.8606572215011));
#177535=CARTESIAN_POINT('Ctrl Pts',(20.6977671458048,-18.1612008067393,
13.8601998304739));
#177536=CARTESIAN_POINT('Ctrl Pts',(20.6933858112382,-18.1504305739998,
13.859491018786));
#177537=CARTESIAN_POINT('Ctrl Pts',(20.6918070586786,-18.146582205526,13.8592381161906));
#177538=CARTESIAN_POINT('Ctrl Pts',(20.6888538588364,-18.1394434754006,
13.8587696972341));
#177539=CARTESIAN_POINT('Ctrl Pts',(20.6874824539807,-18.1361519643077,
13.8585540070002));
#177540=CARTESIAN_POINT('Ctrl Pts',(20.6843576357318,-18.1287051360699,
13.858066660091));
#177541=CARTESIAN_POINT('Ctrl Pts',(20.6825992608731,-18.1245519583559,
13.8577953085805));
#177542=CARTESIAN_POINT('Ctrl Pts',(20.6773530880157,-18.1122702748014,
13.8569941097287));
#177543=CARTESIAN_POINT('Ctrl Pts',(20.6738275549437,-18.1041578570673,
13.8564665012397));
#177544=CARTESIAN_POINT('Ctrl Pts',(20.6473672677725,-18.0443006020077,
13.8525837773986));
#177545=CARTESIAN_POINT('Ctrl Pts',(20.6224142823125,-17.9934671662867,
13.8493429340956));
#177546=CARTESIAN_POINT('Ctrl Pts',(20.5159451807352,-17.7969133354706,
13.8368048508807));
#177547=CARTESIAN_POINT('Ctrl Pts',(20.4193556676389,-17.6600491203108,
13.8280140456728));
#177548=CARTESIAN_POINT('Ctrl Pts',(20.2685601734049,-17.4924674541399,
13.8155119844931));
#177549=CARTESIAN_POINT('Ctrl Pts',(20.2276532489514,-17.4506308247862,
13.8122219975605));
#177550=CARTESIAN_POINT('Ctrl Pts',(20.1589897077629,-17.3859935659781,
13.8068037008979));
#177551=CARTESIAN_POINT('Ctrl Pts',(20.1322929944386,-17.3621106020858,
13.804720521714));
#177552=CARTESIAN_POINT('Ctrl Pts',(20.0966389796344,-17.3318072508283,
13.8019616021526));
#177553=CARTESIAN_POINT('Ctrl Pts',(20.0882184700461,-17.324762506023,13.8013116662425));
#177554=CARTESIAN_POINT('Ctrl Pts',(20.0743897808976,-17.3133748638122,
13.8002467811953));
#177555=CARTESIAN_POINT('Ctrl Pts',(20.0690143150772,-17.3089924289704,
13.7998334439103));
#177556=CARTESIAN_POINT('Ctrl Pts',(20.058604088043,-17.3005901426147,13.7990340764229));
#177557=CARTESIAN_POINT('Ctrl Pts',(20.05357231449,-17.2965666994596,13.7986481971558));
#177558=CARTESIAN_POINT('Ctrl Pts',(20.0419645395485,-17.2873715871934,
13.7977591032985));
#177559=CARTESIAN_POINT('Ctrl Pts',(20.0353761225506,-17.2822158301276,
13.7972552615765));
#177560=CARTESIAN_POINT('Ctrl Pts',(20.0176929791805,-17.2685461356653,
13.7959049842466));
#177561=CARTESIAN_POINT('Ctrl Pts',(20.0065442998312,-17.2601029675608,
13.7950557777646));
#177562=CARTESIAN_POINT('Ctrl Pts',(19.9144915569788,-17.1918137413675,
13.7880600319688));
#177563=CARTESIAN_POINT('Ctrl Pts',(19.8295097320171,-17.1377041814489,
13.7816925998755));
#177564=CARTESIAN_POINT('Ctrl Pts',(19.5902989928113,-17.0083440013616,
13.7640470659696));
#177565=CARTESIAN_POINT('Ctrl Pts',(19.4302591033687,-16.9454443031439,
13.7524857772771));
#177566=CARTESIAN_POINT('Ctrl Pts',(19.2257888824506,-16.8925284821273,
13.7389778823449));
#177567=CARTESIAN_POINT('Ctrl Pts',(19.1869053807888,-16.8836295233524,
13.7364660647257));
#177568=CARTESIAN_POINT('Ctrl Pts',(19.1402539044138,-16.8743316365259,
13.7335381860775));
#177569=CARTESIAN_POINT('Ctrl Pts',(19.1327086109033,-16.8728704919655,
13.7330672954573));
#177570=CARTESIAN_POINT('Ctrl Pts',(19.1210209907743,-16.8706731515228,
13.7323421731953));
#177571=CARTESIAN_POINT('Ctrl Pts',(19.1168842359302,-16.8699081768379,
13.7320863498469));
#177572=CARTESIAN_POINT('Ctrl Pts',(19.1092407733773,-16.8685182868598,
13.7316152309988));
#177573=CARTESIAN_POINT('Ctrl Pts',(19.105734795997,-16.86788989524,13.7313997444462));
#177574=CARTESIAN_POINT('Ctrl Pts',(19.0978461368141,-16.8664965161994,
13.730916249382));
#177575=CARTESIAN_POINT('Ctrl Pts',(19.0934626334226,-16.8657364959759,
13.7306485253506));
#177576=CARTESIAN_POINT('Ctrl Pts',(19.0822404270118,-16.8638271880139,
13.72996545517));
#177577=CARTESIAN_POINT('Ctrl Pts',(19.0753983528898,-16.8626976630058,
13.7295512049085));
#177578=CARTESIAN_POINT('Ctrl Pts',(19.0353995765776,-16.8562961935664,
13.7271417558337));
#177579=CARTESIAN_POINT('Ctrl Pts',(19.0021247723537,-16.851779644938,13.7251864795585));
#177580=CARTESIAN_POINT('Ctrl Pts',(18.9506106108374,-16.8460317795856,
13.722215708549));
#177581=CARTESIAN_POINT('Ctrl Pts',(18.9324407318121,-16.8442420411798,
13.7211786184165));
#177582=CARTESIAN_POINT('Ctrl Pts',(18.8831299528729,-16.840028230316,13.7183878330192));
#177583=CARTESIAN_POINT('Ctrl Pts',(18.851954305638,-16.838057851183,13.7166490020242));
#177584=CARTESIAN_POINT('Ctrl Pts',(18.7822810849243,-16.8352005438811,
13.7127985803021));
#177585=CARTESIAN_POINT('Ctrl Pts',(18.7437799226957,-16.8346725613945,
13.7106950087804));
#177586=CARTESIAN_POINT('Ctrl Pts',(18.5960098586888,-16.8366770974319,
13.7026493547095));
#177587=CARTESIAN_POINT('Ctrl Pts',(18.4870146104425,-16.8466188973424,
13.6967644233398));
#177588=CARTESIAN_POINT('Ctrl Pts',(18.3250242599343,-16.8741510180712,
13.6876274304945));
#177589=CARTESIAN_POINT('Ctrl Pts',(18.2711535560168,-16.8854835897332,
13.684524122855));
#177590=CARTESIAN_POINT('Ctrl Pts',(18.1845501981536,-16.9072583256948,
13.6793864578755));
#177591=CARTESIAN_POINT('Ctrl Pts',(18.1515216202109,-16.9164208832722,
13.6773913608685));
#177592=CARTESIAN_POINT('Ctrl Pts',(18.1083928298295,-16.9295209732093,
13.6747330177077));
#177593=CARTESIAN_POINT('Ctrl Pts',(18.0980786971841,-16.932740275435,13.6740932479001));
#177594=CARTESIAN_POINT('Ctrl Pts',(18.0812217041842,-16.9381437317735,
13.6730408310188));
#177595=CARTESIAN_POINT('Ctrl Pts',(18.0746639943558,-16.9402811820502,
13.6726297235628));
#177596=CARTESIAN_POINT('Ctrl Pts',(18.0619874554704,-16.9444816724802,
13.6718316846659));
#177597=CARTESIAN_POINT('Ctrl Pts',(18.0558673829804,-16.9465407389742,
13.6714448882269));
#177598=CARTESIAN_POINT('Ctrl Pts',(18.0417538798914,-16.9513611448833,
13.6705493530508));
#177599=CARTESIAN_POINT('Ctrl Pts',(18.0337674242931,-16.954142433484,13.6700399574625));
#177600=CARTESIAN_POINT('Ctrl Pts',(18.0123241714089,-16.9617544328562,
13.668665048468));
#177601=CARTESIAN_POINT('Ctrl Pts',(17.998899472983,-16.9666736745448,13.6677966030124));
#177602=CARTESIAN_POINT('Ctrl Pts',(17.8756712302297,-17.0132496851991,
13.6597526956773));
#177603=CARTESIAN_POINT('Ctrl Pts',(17.7694802222011,-17.0638329686308,
13.6522722424118));
#177604=CARTESIAN_POINT('Ctrl Pts',(17.5265488143714,-17.2054114947464,
13.633902001293));
#177605=CARTESIAN_POINT('Ctrl Pts',(17.3951038112648,-17.3040112030056,
13.6228709597717));
#177606=CARTESIAN_POINT('Ctrl Pts',(17.2538231638002,-17.4381540700932,
13.6105089084557));
#177607=CARTESIAN_POINT('Ctrl Pts',(17.2317792610491,-17.460026121755,13.6085649687121));
#177608=CARTESIAN_POINT('Ctrl Pts',(17.205268564518,-17.4875136949609,13.606217151333));
#177609=CARTESIAN_POINT('Ctrl Pts',(17.2003398493186,-17.4926760177962,
13.6057802224147));
#177610=CARTESIAN_POINT('Ctrl Pts',(17.1926298765882,-17.5008336252696,
13.60509619059));
#177611=CARTESIAN_POINT('Ctrl Pts',(17.1898310778336,-17.503812151355,13.6048477657558));
#177612=CARTESIAN_POINT('Ctrl Pts',(17.1846001254261,-17.5094114197576,
13.6043832775744));
#177613=CARTESIAN_POINT('Ctrl Pts',(17.1821660131123,-17.5120301876336,
13.6041670672029));
#177614=CARTESIAN_POINT('Ctrl Pts',(17.1766043188343,-17.5180442819201,
13.6036728681127));
#177615=CARTESIAN_POINT('Ctrl Pts',(17.1734812054159,-17.5214436740196,
13.6033952202802));
#177616=CARTESIAN_POINT('Ctrl Pts',(17.1638449915378,-17.5320014398754,
13.6025380296285));
#177617=CARTESIAN_POINT('Ctrl Pts',(17.1573697342568,-17.5391943960583,
13.6019612789278));
#177618=CARTESIAN_POINT('Ctrl Pts',(17.0888259491366,-17.6163935292043,
13.5958448821422));
#177619=CARTESIAN_POINT('Ctrl Pts',(17.0314058435558,-17.6904058048352,
13.5906201640413));
#177620=CARTESIAN_POINT('Ctrl Pts',(16.9052207571342,-17.8774357311332,
13.5782429453261));
#177621=CARTESIAN_POINT('Ctrl Pts',(16.8417781178672,-17.9935541008624,
13.5711935441839));
#177622=CARTESIAN_POINT('Ctrl Pts',(16.7738052627277,-18.1514291303372,
13.5616456907613));
#177623=CARTESIAN_POINT('Ctrl Pts',(16.7590846233678,-18.1884650609054,
13.5594100858738));
#177624=CARTESIAN_POINT('Ctrl Pts',(16.7454193670368,-18.225889769936,13.5571445045843));
#177625=CARTESIAN_POINT('',(16.6170007998506,-18.9500893124935,14.0892703911058));
#177626=CARTESIAN_POINT('Ctrl Pts',(16.7454194046024,-18.225889667056,13.3344632333882));
#177627=CARTESIAN_POINT('Ctrl Pts',(16.7539003524645,-18.2026631027393,
13.336089857378));
#177628=CARTESIAN_POINT('Ctrl Pts',(16.7627902765797,-18.1795795115226,
13.3377116760456));
#177629=CARTESIAN_POINT('Ctrl Pts',(16.7783264505047,-18.1412559718137,
13.3404079872272));
#177630=CARTESIAN_POINT('Ctrl Pts',(16.7847480723209,-18.1259359259581,
13.3414868650764));
#177631=CARTESIAN_POINT('Ctrl Pts',(16.8125073103354,-18.0618374645365,
13.3460009929237));
#177632=CARTESIAN_POINT('Ctrl Pts',(16.8355026388732,-18.0137930414874,
13.349385222995));
#177633=CARTESIAN_POINT('Ctrl Pts',(16.8643428909334,-17.9589505434368,
13.3532075465039));
#177634=CARTESIAN_POINT('Ctrl Pts',(16.8684462592698,-17.9512631838952,
13.3537423619827));
#177635=CARTESIAN_POINT('Ctrl Pts',(16.874731891055,-17.9396605383436,13.3545478473222));
#177636=CARTESIAN_POINT('Ctrl Pts',(16.8768792573934,-17.935726594463,13.35482065036));
#177637=CARTESIAN_POINT('Ctrl Pts',(16.8807565591158,-17.9286767618996,
13.3553089445088));
#177638=CARTESIAN_POINT('Ctrl Pts',(16.8824818761278,-17.9255584096634,
13.3555247232875));
#177639=CARTESIAN_POINT('Ctrl Pts',(16.8862483454407,-17.9187912591001,
13.3559925282457));
#177640=CARTESIAN_POINT('Ctrl Pts',(16.8882924278162,-17.9151441576208,
13.3562443630418));
#177641=CARTESIAN_POINT('Ctrl Pts',(16.8940655506734,-17.9049147822005,
13.356949974689));
#177642=CARTESIAN_POINT('Ctrl Pts',(16.8978191321277,-17.8983463303686,
13.3574022033368));
#177643=CARTESIAN_POINT('Ctrl Pts',(16.9204919363382,-17.8591599599498,
13.3600958513959));
#177644=CARTESIAN_POINT('Ctrl Pts',(16.9402459402481,-17.8270299474275,
13.3622866583483));
#177645=CARTESIAN_POINT('Ctrl Pts',(17.0081356277537,-17.7229463384696,
13.3693824529943));
#177646=CARTESIAN_POINT('Ctrl Pts',(17.0598276861012,-17.653412241126,13.374123014618));
#177647=CARTESIAN_POINT('Ctrl Pts',(17.2291757705467,-17.45259621933,13.3884176312927));
#177648=CARTESIAN_POINT('Ctrl Pts',(17.3590578341418,-17.3326683386654,
13.3978831087856));
#177649=CARTESIAN_POINT('Ctrl Pts',(17.5209471697267,-17.2168578287132,
13.4094500361173));
#177650=CARTESIAN_POINT('Ctrl Pts',(17.5398248787797,-17.2038120115654,
13.410794386808));
#177651=CARTESIAN_POINT('Ctrl Pts',(17.5668447374941,-17.1857812759897,
13.4127140830162));
#177652=CARTESIAN_POINT('Ctrl Pts',(17.5748146827075,-17.1805403240585,
13.4132797831267));
#177653=CARTESIAN_POINT('Ctrl Pts',(17.5878261061958,-17.1721095560344,
13.4142025594507));
#177654=CARTESIAN_POINT('Ctrl Pts',(17.5928461842817,-17.1688868361464,
13.4145584026044));
#177655=CARTESIAN_POINT('Ctrl Pts',(17.603386238513,-17.1621832192265,13.4153051747859));
#177656=CARTESIAN_POINT('Ctrl Pts',(17.6089088151235,-17.1587065464249,
13.4156962553992));
#177657=CARTESIAN_POINT('Ctrl Pts',(17.6220913770569,-17.1504924835205,
13.4166293504809));
#177658=CARTESIAN_POINT('Ctrl Pts',(17.6297656466736,-17.1457783616835,
13.4171722146517));
#177659=CARTESIAN_POINT('Ctrl Pts',(17.6557515255351,-17.1300433596053,
13.4190094146126));
#177660=CARTESIAN_POINT('Ctrl Pts',(17.6741994151492,-17.1192511246894,
13.4203120408752));
#177661=CARTESIAN_POINT('Ctrl Pts',(17.7757270925724,-17.0619016870768,
13.4274744457338));
#177662=CARTESIAN_POINT('Ctrl Pts',(17.8617020662172,-17.020717865647,13.4335232534566));
#177663=CARTESIAN_POINT('Ctrl Pts',(18.1086037907643,-16.9223038927295,
13.4507947272331));
#177664=CARTESIAN_POINT('Ctrl Pts',(18.2741027520591,-16.8785299435595,
13.4623042606654));
#177665=CARTESIAN_POINT('Ctrl Pts',(18.4794996029676,-16.8500313296989,
13.4755392909284));
#177666=CARTESIAN_POINT('Ctrl Pts',(18.516071976282,-16.8459253344735,13.4778537099786));
#177667=CARTESIAN_POINT('Ctrl Pts',(18.5598511689017,-16.8421629931504,
13.4805595846343));
#177668=CARTESIAN_POINT('Ctrl Pts',(18.5669702929428,-16.8415874594942,
13.4809975624706));
#177669=CARTESIAN_POINT('Ctrl Pts',(18.5785918334233,-16.8407071108761,
13.4817090635648));
#177670=CARTESIAN_POINT('Ctrl Pts',(18.5830924853179,-16.8403806486992,
13.4819837564659));
#177671=CARTESIAN_POINT('Ctrl Pts',(18.5911516255582,-16.8398219634576,
13.482474077201));
#177672=CARTESIAN_POINT('Ctrl Pts',(18.5947096753999,-16.8395843396214,
13.482690003241));
#177673=CARTESIAN_POINT('Ctrl Pts',(18.6024176333088,-16.8390891244443,
13.4831565833469));
#177674=CARTESIAN_POINT('Ctrl Pts',(18.6065676917752,-16.8388347687014,
13.4834070543531));
#177675=CARTESIAN_POINT('Ctrl Pts',(18.6181652197954,-16.8381582495792,
13.4841050025983));
#177676=CARTESIAN_POINT('Ctrl Pts',(18.6256142956396,-16.837763214544,13.4845509852218));
#177677=CARTESIAN_POINT('Ctrl Pts',(18.6689406698259,-16.8356951427539,
13.4871323550971));
#177678=CARTESIAN_POINT('Ctrl Pts',(18.704856114594,-16.8348958587633,13.4892219140928));
#177679=CARTESIAN_POINT('Ctrl Pts',(18.8205015405215,-16.8352660586759,
13.4958377363242));
#177680=CARTESIAN_POINT('Ctrl Pts',(18.9001547247206,-16.840024695492,13.5002239731848));
#177681=CARTESIAN_POINT('Ctrl Pts',(19.1643166047464,-16.870848103593,13.514724185321));
#177682=CARTESIAN_POINT('Ctrl Pts',(19.345600774252,-16.9167348744402,13.524680855757));
#177683=CARTESIAN_POINT('Ctrl Pts',(19.5390203102987,-16.9939097633066,
13.5367933177697));
#177684=CARTESIAN_POINT('Ctrl Pts',(19.5593680915753,-17.0023993910069,
13.538085782113));
#177685=CARTESIAN_POINT('Ctrl Pts',(19.5873252906305,-17.0145799775871,
13.5398884606527));
#177686=CARTESIAN_POINT('Ctrl Pts',(19.5950511931441,-17.0180012320284,
13.5403894968882));
#177687=CARTESIAN_POINT('Ctrl Pts',(19.6082967266698,-17.023961840106,13.5412535241017));
#177688=CARTESIAN_POINT('Ctrl Pts',(19.6138263266479,-17.0264788897479,
13.5416157469552));
#177689=CARTESIAN_POINT('Ctrl Pts',(19.6252042283873,-17.0317173043175,
13.5423642410518));
#177690=CARTESIAN_POINT('Ctrl Pts',(19.6310510747576,-17.0344416629785,
13.5427506127031));
#177691=CARTESIAN_POINT('Ctrl Pts',(19.644629325278,-17.040844188729,13.5436519867897));
#177692=CARTESIAN_POINT('Ctrl Pts',(19.652351008045,-17.0445426018729,13.5441676875279));
#177693=CARTESIAN_POINT('Ctrl Pts',(19.6769987557534,-17.0565323577941,
13.545823911042));
#177694=CARTESIAN_POINT('Ctrl Pts',(19.6938362474643,-17.0650027615292,
13.5469706590549));
#177695=CARTESIAN_POINT('Ctrl Pts',(19.7774011679847,-17.1084494123327,
13.5527406789516));
#177696=CARTESIAN_POINT('Ctrl Pts',(19.8423343265186,-17.1467416757843,
13.5574803603144));
#177697=CARTESIAN_POINT('Ctrl Pts',(19.9960274933769,-17.248799067349,13.5693363841238));
#177698=CARTESIAN_POINT('Ctrl Pts',(20.0821579942293,-17.3161291732635,
13.5765525554743));
#177699=CARTESIAN_POINT('Ctrl Pts',(20.1738253381538,-17.3999629311809,
13.5847586850779));
#177700=CARTESIAN_POINT('Ctrl Pts',(20.184836236259,-17.4102509002412,13.5857535790107));
#177701=CARTESIAN_POINT('Ctrl Pts',(20.2707592430541,-17.4922682344573,
13.5935857163402));
#177702=CARTESIAN_POINT('Ctrl Pts',(20.340427471791,-17.5693063638114,13.6003591315249));
#177703=CARTESIAN_POINT('Ctrl Pts',(20.4101260258063,-17.6587929804181,
13.6073671004742));
#177704=CARTESIAN_POINT('Ctrl Pts',(20.4160264505532,-17.6664768077909,
13.6079623337494));
#177705=CARTESIAN_POINT('Ctrl Pts',(20.4246614678704,-17.6778830008016,
13.6088360209613));
#177706=CARTESIAN_POINT('Ctrl Pts',(20.4274368628119,-17.6815741189699,
13.6091172361096));
#177707=CARTESIAN_POINT('Ctrl Pts',(20.4323396252473,-17.6881391288657,
13.6096146772753));
#177708=CARTESIAN_POINT('Ctrl Pts',(20.4344718103382,-17.6910093548351,
13.609831237707));
#177709=CARTESIAN_POINT('Ctrl Pts',(20.4390249884247,-17.6971711337458,
13.6102941681123));
#177710=CARTESIAN_POINT('Ctrl Pts',(20.441443720334,-17.7004642884526,13.6105403815742));
#177711=CARTESIAN_POINT('Ctrl Pts',(20.4480580007005,-17.7095246350391,
13.6112145576049));
#177712=CARTESIAN_POINT('Ctrl Pts',(20.4522340089326,-17.7153061186601,
13.6116411863517));
#177713=CARTESIAN_POINT('Ctrl Pts',(20.4743893825871,-17.7463080353882,
13.6139105344812));
#177714=CARTESIAN_POINT('Ctrl Pts',(20.4918438694643,-17.7719010739727,
13.615719409072));
#177715=CARTESIAN_POINT('Ctrl Pts',(20.5978754531955,-17.9349481219017,
13.6269059288837));
#177716=CARTESIAN_POINT('Ctrl Pts',(20.6708474847609,-18.0819078246826,
13.6355483597946));
#177717=CARTESIAN_POINT('Ctrl Pts',(20.7660118637535,-18.3466229109875,
13.6509435195264));
#177718=CARTESIAN_POINT('Ctrl Pts',(20.796527315069,-18.4605436339403,13.6575138956757));
#177719=CARTESIAN_POINT('Ctrl Pts',(20.8199515596796,-18.5904759727044,
13.6652483585029));
#177720=CARTESIAN_POINT('Ctrl Pts',(20.8223461923881,-18.6045756234303,
13.6660905375797));
#177721=CARTESIAN_POINT('Ctrl Pts',(20.8259293818693,-18.6270507732195,
13.667437990705));
#177722=CARTESIAN_POINT('Ctrl Pts',(20.8272109399408,-18.635411155505,13.6679403175115));
#177723=CARTESIAN_POINT('Ctrl Pts',(20.8293825006736,-18.6501674742287,
13.668828958476));
#177724=CARTESIAN_POINT('Ctrl Pts',(20.8302934088461,-18.6565602593672,
13.6692146055066));
#177725=CARTESIAN_POINT('Ctrl Pts',(20.8321166991622,-18.669789293524,13.6700140707878));
#177726=CARTESIAN_POINT('Ctrl Pts',(20.833024949567,-18.6766260261083,13.6704280148275));
#177727=CARTESIAN_POINT('Ctrl Pts',(20.8352700542355,-18.6941825088929,
13.6714930703164));
#177728=CARTESIAN_POINT('Ctrl Pts',(20.8365582807662,-18.7049081774827,
13.6721457087488));
#177729=CARTESIAN_POINT('Ctrl Pts',(20.8415887217315,-18.7496830985969,
13.6748786940828));
#177730=CARTESIAN_POINT('Ctrl Pts',(20.844586174763,-18.7838092388975,13.6769823067786));
#177731=CARTESIAN_POINT('Ctrl Pts',(20.8502353808129,-18.8728736752039,
13.6825292345993));
#177732=CARTESIAN_POINT('Ctrl Pts',(20.8515764257692,-18.9278664735895,
13.6860108052008));
#177733=CARTESIAN_POINT('Ctrl Pts',(20.8491826972318,-19.0921357874228,
13.6965697449011));
#177734=CARTESIAN_POINT('Ctrl Pts',(20.8391285296679,-19.2011310634843,
13.7037955397244));
#177735=CARTESIAN_POINT('Ctrl Pts',(20.8142524002979,-19.3465947782513,
13.713544165535));
#177736=CARTESIAN_POINT('Ctrl Pts',(20.8067752500602,-19.38415500747,13.7160696795729));
#177737=CARTESIAN_POINT('Ctrl Pts',(20.7910457636762,-19.453315066172,13.7207164573003));
#177738=CARTESIAN_POINT('Ctrl Pts',(20.7830729771046,-19.4849673063677,
13.7228417176583));
#177739=CARTESIAN_POINT('Ctrl Pts',(20.7735175281082,-19.5195099180314,
13.7251514085116));
#177740=CARTESIAN_POINT('Ctrl Pts',(20.7726567503308,-19.5225943471818,
13.7253575630732));
#177741=CARTESIAN_POINT('Ctrl Pts',(20.7592838654499,-19.5700969064179,
13.7285310649638));
#177742=CARTESIAN_POINT('Ctrl Pts',(20.7453286058861,-19.6141000401863,
13.7314516379822));
#177743=CARTESIAN_POINT('Ctrl Pts',(20.7273949441287,-19.6648282596846,
13.7347686199128));
#177744=CARTESIAN_POINT('Ctrl Pts',(20.7248058168856,-19.6720275929376,
13.7352381692315));
#177745=CARTESIAN_POINT('Ctrl Pts',(20.7205920439777,-19.6835479190047,
13.735987437124));
#177746=CARTESIAN_POINT('Ctrl Pts',(20.7189922226535,-19.6878778322058,
13.7362685712276));
#177747=CARTESIAN_POINT('Ctrl Pts',(20.7161250466301,-19.6955604519296,
13.7367664961684));
#177748=CARTESIAN_POINT('Ctrl Pts',(20.7148633254281,-19.6989152112827,
13.7369836186124));
#177749=CARTESIAN_POINT('Ctrl Pts',(20.7121611550301,-19.7060449384769,
13.7374443961343));
#177750=CARTESIAN_POINT('Ctrl Pts',(20.7107184205992,-19.7098189828746,
13.7376879120659));
#177751=CARTESIAN_POINT('Ctrl Pts',(20.7067732930654,-19.7200511064626,
13.7383471234583));
#177752=CARTESIAN_POINT('Ctrl Pts',(20.7042499732011,-19.7265011388612,
13.7387615821668));
#177753=CARTESIAN_POINT('Ctrl Pts',(20.6912698550748,-19.7592065371379,
13.7408581462147));
#177754=CARTESIAN_POINT('Ctrl Pts',(20.6803191778902,-19.785264371617,13.7425122201924));
#177755=CARTESIAN_POINT('Ctrl Pts',(20.6466749328626,-19.8610376362878,
13.7472956561698));
#177756=CARTESIAN_POINT('Ctrl Pts',(20.6225736085474,-19.9101050957269,
13.7503594737831));
#177757=CARTESIAN_POINT('Ctrl Pts',(20.5294284003924,-20.0825302940906,
13.7611898315668));
#177758=CARTESIAN_POINT('Ctrl Pts',(20.4499757946822,-20.1998345045874,
13.7687031809662));
#177759=CARTESIAN_POINT('Ctrl Pts',(20.3021585790556,-20.37697605724,13.7814809195929));
#177760=CARTESIAN_POINT('Ctrl Pts',(20.2406099228957,-20.4418999430942,
13.786537736569));
#177761=CARTESIAN_POINT('Ctrl Pts',(20.1651123771409,-20.5120621955398,
13.7925804196745));
#177762=CARTESIAN_POINT('Ctrl Pts',(20.1549867987538,-20.5212906660536,
13.7933876540355));
#177763=CARTESIAN_POINT('Ctrl Pts',(20.1385972027527,-20.5359394865182,
13.7946895717616));
#177764=CARTESIAN_POINT('Ctrl Pts',(20.1323895998671,-20.5414225753209,
13.7951816147904));
#177765=CARTESIAN_POINT('Ctrl Pts',(20.1213060435957,-20.5510973342095,
13.7960583544532));
#177766=CARTESIAN_POINT('Ctrl Pts',(20.1164428430365,-20.5553035043939,
13.79644244134));
#177767=CARTESIAN_POINT('Ctrl Pts',(20.1062656726431,-20.5640249841146,
13.7972449994028));
#177768=CARTESIAN_POINT('Ctrl Pts',(20.1009484110886,-20.5685363173577,
13.7976636277541));
#177769=CARTESIAN_POINT('Ctrl Pts',(20.0870716703492,-20.5801923614128,
13.7987544329902));
#177770=CARTESIAN_POINT('Ctrl Pts',(20.0784779469333,-20.587295800039,13.7994282817828));
#177771=CARTESIAN_POINT('Ctrl Pts',(20.0408170896054,-20.6179281477777,
13.8023744236567));
#177772=CARTESIAN_POINT('Ctrl Pts',(20.0111869455471,-20.6407512326211,
13.8046747616221));
#177773=CARTESIAN_POINT('Ctrl Pts',(19.9307600055691,-20.699373690697,13.8108768734502));
#177774=CARTESIAN_POINT('Ctrl Pts',(19.8789680575382,-20.7337396910258,
13.8148291357925));
#177775=CARTESIAN_POINT('Ctrl Pts',(19.7231172909987,-20.8275489928654,
13.8265844553654));
#177776=CARTESIAN_POINT('Ctrl Pts',(19.6154377901442,-20.8804970835454,
13.8345488982109));
#177777=CARTESIAN_POINT('Ctrl Pts',(19.4135659844437,-20.9593058001976,
13.8488180310605));
#177778=CARTESIAN_POINT('Ctrl Pts',(19.3209364219741,-20.9883193738169,
13.8551280801419));
#177779=CARTESIAN_POINT('Ctrl Pts',(19.2172086718811,-21.0131385966935,
13.8617177281017));
#177780=CARTESIAN_POINT('Ctrl Pts',(19.2077671315104,-21.0153292632683,
13.8623132357389));
#177781=CARTESIAN_POINT('Ctrl Pts',(19.1938042095478,-21.0184681036448,
13.8631872472829));
#177782=CARTESIAN_POINT('Ctrl Pts',(19.1892943905398,-21.0194664092496,
13.8634685152981));
#177783=CARTESIAN_POINT('Ctrl Pts',(19.1812876927908,-21.0212113243425,
13.8639660149026));
#177784=CARTESIAN_POINT('Ctrl Pts',(19.1777921572663,-21.0219638418914,
13.8641825811992));
#177785=CARTESIAN_POINT('Ctrl Pts',(19.1702986076366,-21.0235571957604,
13.8646454853417));
#177786=CARTESIAN_POINT('Ctrl Pts',(19.166300072379,-21.0243953142204,13.8648916668787));
#177787=CARTESIAN_POINT('Ctrl Pts',(19.1553171893943,-21.0266642266586,
13.8655656654203));
#177788=CARTESIAN_POINT('Ctrl Pts',(19.1483279269635,-21.0280713378125,
13.8659921497727));
#177789=CARTESIAN_POINT('Ctrl Pts',(19.1109706666151,-21.0353961071367,
13.8682593507968));
#177790=CARTESIAN_POINT('Ctrl Pts',(19.0804810831658,-21.0406831519165,
13.870066298496));
#177791=CARTESIAN_POINT('Ctrl Pts',(18.9878385464108,-21.0546631670935,
13.8754553235058));
#177792=CARTESIAN_POINT('Ctrl Pts',(18.9254019540112,-21.0612635787971,
13.8789505168442));
#177793=CARTESIAN_POINT('Ctrl Pts',(18.704030075372,-21.0747528409897,13.8911389494923));
#177794=CARTESIAN_POINT('Ctrl Pts',(18.5447211456008,-21.0665098111604,
13.8995812656302));
#177795=CARTESIAN_POINT('Ctrl Pts',(18.3258285304965,-21.0302289489533,
13.9120639289613));
#177796=CARTESIAN_POINT('Ctrl Pts',(18.2643148615901,-21.0171959442851,
13.9156661783047));
#177797=CARTESIAN_POINT('Ctrl Pts',(18.1914005345203,-20.9983211877463,
13.920089459441));
#177798=CARTESIAN_POINT('Ctrl Pts',(18.1793533099789,-20.995088745658,13.9208253388945));
#177799=CARTESIAN_POINT('Ctrl Pts',(18.1596261795417,-20.9896083371777,
13.9220389228766));
#177800=CARTESIAN_POINT('Ctrl Pts',(18.151929102011,-20.987422926173,13.9225145948675));
#177801=CARTESIAN_POINT('Ctrl Pts',(18.1381184264747,-20.9834169535159,
13.9233720419129));
#177802=CARTESIAN_POINT('Ctrl Pts',(18.1320002898861,-20.981612287198,13.9237532942526));
#177803=CARTESIAN_POINT('Ctrl Pts',(18.118993107782,-20.9777115723511,13.92456686861));
#177804=CARTESIAN_POINT('Ctrl Pts',(18.1121064272423,-20.9756079743864,
13.924999433884));
#177805=CARTESIAN_POINT('Ctrl Pts',(18.0936032231324,-20.9698526324287,
13.9261666158466));
#177806=CARTESIAN_POINT('Ctrl Pts',(18.0820073843388,-20.9661357693647,
13.9269033630824));
#177807=CARTESIAN_POINT('Ctrl Pts',(18.0250665895771,-20.9473410515868,
13.9305476833004));
#177808=CARTESIAN_POINT('Ctrl Pts',(17.980212055019,-20.9308318896352,13.9335022185114));
#177809=CARTESIAN_POINT('Ctrl Pts',(17.7804986855081,-20.8495496704731,
13.9470494161377));
#177810=CARTESIAN_POINT('Ctrl Pts',(17.633134541706,-20.7680226370081,13.958197698942));
#177811=CARTESIAN_POINT('Ctrl Pts',(17.4168216353448,-20.6122663317817,
13.9757560270314));
#177812=CARTESIAN_POINT('Ctrl Pts',(17.3408006318111,-20.5490107349291,
13.982190485097));
#177813=CARTESIAN_POINT('Ctrl Pts',(17.2624671798305,-20.473963910728,13.9888929466025));
#177814=CARTESIAN_POINT('Ctrl Pts',(17.2555127344352,-20.4672090285377,
13.9894886179829));
#177815=CARTESIAN_POINT('Ctrl Pts',(17.2453133412618,-20.4571652305694,
13.9903628230858));
#177816=CARTESIAN_POINT('Ctrl Pts',(17.2420324763639,-20.4539131960833,
13.9906441226462));
#177817=CARTESIAN_POINT('Ctrl Pts',(17.236230998062,-20.4481249286493,13.9911416571258));
#177818=CARTESIAN_POINT('Ctrl Pts',(17.2337061417771,-20.4455930252082,
13.991358226927));
#177819=CARTESIAN_POINT('Ctrl Pts',(17.2283104489712,-20.4401547848357,
13.9918211154224));
#177820=CARTESIAN_POINT('Ctrl Pts',(17.225441614127,-20.4372465400626,13.9920672779286));
#177821=CARTESIAN_POINT('Ctrl Pts',(17.2195717244196,-20.4312614612724,
13.9925710964168));
#177822=CARTESIAN_POINT('Ctrl Pts',(17.2165715832354,-20.4281837532667,
13.9928286817238));
#177823=CARTESIAN_POINT('Ctrl Pts',(17.2028281910154,-20.4139988633756,
13.9940091492461));
#177824=CARTESIAN_POINT('Ctrl Pts',(17.1921970585629,-20.4027830665149,
13.9949236799429));
#177825=CARTESIAN_POINT('Ctrl Pts',(17.1270839017022,-20.3325647599154,
14.0005412506516));
#177826=CARTESIAN_POINT('Ctrl Pts',(17.0758674040217,-20.2706119379657,
14.0050328569994));
#177827=CARTESIAN_POINT('Ctrl Pts',(16.9870844250608,-20.1498376664508,
14.0132735203915));
#177828=CARTESIAN_POINT('Ctrl Pts',(16.948665264207,-20.0917847940165,14.0170365238758));
#177829=CARTESIAN_POINT('Ctrl Pts',(16.8366942173446,-19.9029974988654,
14.0289657710074));
#177830=CARTESIAN_POINT('Ctrl Pts',(16.7741390010244,-19.7663108177587,
14.0371977909662));
#177831=CARTESIAN_POINT('Ctrl Pts',(16.7220478750258,-19.6107399544399,
14.0468105562725));
#177832=CARTESIAN_POINT('Ctrl Pts',(16.7176849721947,-19.5972622527926,
14.0476448783759));
#177833=CARTESIAN_POINT('Ctrl Pts',(16.7109454564642,-19.5757068140997,
14.0489821048932));
#177834=CARTESIAN_POINT('Ctrl Pts',(16.7084811540771,-19.5676567856875,
14.0494821324417));
#177835=CARTESIAN_POINT('Ctrl Pts',(16.7042134851154,-19.5534127694799,
14.0503680983448));
#177836=CARTESIAN_POINT('Ctrl Pts',(16.7023902813248,-19.547224801956,14.0507533824506));
#177837=CARTESIAN_POINT('Ctrl Pts',(16.6986719539726,-19.5343886454759,
14.0515534693251));
#177838=CARTESIAN_POINT('Ctrl Pts',(16.6967810570793,-19.5277393213656,
14.0519684046648));
#177839=CARTESIAN_POINT('Ctrl Pts',(16.6919990651489,-19.5106049375816,
14.0530389203583));
#177840=CARTESIAN_POINT('Ctrl Pts',(16.6891561702079,-19.5001067405812,
14.0536960580349));
#177841=CARTESIAN_POINT('Ctrl Pts',(16.6831808524464,-19.4773474686982,
14.0551235042638));
#177842=CARTESIAN_POINT('Ctrl Pts',(16.680077234064,-19.4650793306029,14.0558947171782));
#177843=CARTESIAN_POINT('Ctrl Pts',(16.6713661333626,-19.4292994480852,
14.0581493239078));
#177844=CARTESIAN_POINT('Ctrl Pts',(16.6660512435801,-19.4057191824863,
14.0596419383516));
#177845=CARTESIAN_POINT('Ctrl Pts',(16.6316557511639,-19.2399329757323,
14.07018533815));
#177846=CARTESIAN_POINT('Ctrl Pts',(16.6168699503902,-19.095183031562,14.079683056516));
#177847=CARTESIAN_POINT('Ctrl Pts',(16.6170008616905,-18.9500899223173,
14.0892704589852));
#177848=CARTESIAN_POINT('Ctrl Pts',(16.6170008622343,-18.9500893196667,
14.0892704988069));
#177849=CARTESIAN_POINT('Ctrl Pts',(16.6171115220882,-18.8274802096574,
14.0973722129365));
#177850=CARTESIAN_POINT('Ctrl Pts',(16.6278735782882,-18.7050980287736,
14.1054939065436));
#177851=CARTESIAN_POINT('Ctrl Pts',(16.6513555158941,-18.5719488797031,
14.1139585263025));
#177852=CARTESIAN_POINT('Ctrl Pts',(16.653648125981,-18.5595933258764,14.1147402671926));
#177853=CARTESIAN_POINT('Ctrl Pts',(16.6573287573147,-18.5406969010199,
14.1159293732425));
#177854=CARTESIAN_POINT('Ctrl Pts',(16.658637933201,-18.5341411915676,14.1163407091571));
#177855=CARTESIAN_POINT('Ctrl Pts',(16.6608486766872,-18.5233376087066,
14.1170164731497));
#177856=CARTESIAN_POINT('Ctrl Pts',(16.6617322884575,-18.51908616617,14.117281862338));
#177857=CARTESIAN_POINT('Ctrl Pts',(16.6634789761774,-18.5108099811438,
14.1177973993164));
#177858=CARTESIAN_POINT('Ctrl Pts',(16.6643407213338,-18.506784980344,14.1180476200037));
#177859=CARTESIAN_POINT('Ctrl Pts',(16.6659719864128,-18.4992728339622,
14.1185136513447));
#177860=CARTESIAN_POINT('Ctrl Pts',(16.666738581683,-18.495785159794,14.1187296198732));
#177861=CARTESIAN_POINT('Ctrl Pts',(16.6685067296667,-18.4878368283752,
14.1192209191906));
#177862=CARTESIAN_POINT('Ctrl Pts',(16.669513906797,-18.4833774743403,14.1194959240696));
#177863=CARTESIAN_POINT('Ctrl Pts',(16.6726472977603,-18.4697103152121,
14.120336915301));
#177864=CARTESIAN_POINT('Ctrl Pts',(16.6748207595074,-18.4605133103523,
14.1209002596648));
#177865=CARTESIAN_POINT('Ctrl Pts',(16.6956478234693,-18.3749475836915,
14.1261199387586));
#177866=CARTESIAN_POINT('Ctrl Pts',(16.7184739276668,-18.2996845882871,
14.1305523024423));
#177867=CARTESIAN_POINT('Ctrl Pts',(16.7454193947488,-18.2258896940418,
14.1348940370926));
#177868=CARTESIAN_POINT('Origin',(18.734,-18.952,0.));
#177869=CARTESIAN_POINT('',(16.7454193692319,-18.2258897639242,15.1555945373748));
#177870=CARTESIAN_POINT('',(16.7454193926287,-18.2258896998479,14.9318514575852));
#177871=CARTESIAN_POINT('',(16.7454193692319,-18.2258897639242,0.));
#177872=CARTESIAN_POINT('',(16.6156459649053,-18.9502594248307,15.110942953281));
#177873=CARTESIAN_POINT('Ctrl Pts',(16.6170007251258,-18.9502478064743,
15.1109437209775));
#177874=CARTESIAN_POINT('Ctrl Pts',(16.6170993834536,-18.8310488678702,
15.1181312937192));
#177875=CARTESIAN_POINT('Ctrl Pts',(16.6272689227094,-18.7122546433194,
15.1253188664609));
#177876=CARTESIAN_POINT('Ctrl Pts',(16.6472858251195,-18.5951905938001,
15.1325064392026));
#177877=CARTESIAN_POINT('Ctrl Pts',(16.6595036684846,-18.5237374692653,
15.1368935634506));
#177878=CARTESIAN_POINT('Ctrl Pts',(16.6754196380939,-18.4527731733662,
15.1412806876986));
#177879=CARTESIAN_POINT('Ctrl Pts',(16.6949811994244,-18.3827098008052,
15.1456678119466));
#177880=CARTESIAN_POINT('Ctrl Pts',(16.709735150403,-18.329865779477,15.1489767204226));
#177881=CARTESIAN_POINT('Ctrl Pts',(16.7265618805371,-18.277534314435,15.1522856288987));
#177882=CARTESIAN_POINT('Ctrl Pts',(16.7454193692319,-18.2258897639242,
15.1555945373748));
#177883=CARTESIAN_POINT('Ctrl Pts',(16.743090036011,-18.2250592052755,14.3554399658108));
#177884=CARTESIAN_POINT('Ctrl Pts',(16.7690653566902,-18.1521457215081,
14.3601105102452));
#177885=CARTESIAN_POINT('Ctrl Pts',(17.0725680384113,-17.4332647782197,
14.40717299024));
#177886=CARTESIAN_POINT('Ctrl Pts',(18.4531255181642,-16.4645434415688,
14.4966274057954));
#177887=CARTESIAN_POINT('Ctrl Pts',(20.6735252872927,-17.3694159533935,
14.6238032124768));
#177888=CARTESIAN_POINT('Ctrl Pts',(21.1145309858464,-19.7262111017336,
14.7509790191583));
#177889=CARTESIAN_POINT('Ctrl Pts',(19.3715472573024,-21.3727156171947,
14.8781548258396));
#177890=CARTESIAN_POINT('Ctrl Pts',(17.1752233382973,-20.8308254969318,
14.9981428038806));
#177891=CARTESIAN_POINT('Ctrl Pts',(16.6208559183895,-19.5344638852643,
15.075738846361));
#177892=CARTESIAN_POINT('Ctrl Pts',(16.6156459649053,-18.9502594248307,
15.110942953281));
#177893=CARTESIAN_POINT('Ctrl Pts',(16.7454193947488,-18.2258896940418,
14.1348940370926));
#177894=CARTESIAN_POINT('Ctrl Pts',(16.7604972189655,-18.184596424189,14.1373235333657));
#177895=CARTESIAN_POINT('Ctrl Pts',(16.7768648746395,-18.1437628265383,
14.1397244619261));
#177896=CARTESIAN_POINT('Ctrl Pts',(16.8230771617196,-18.0381372392333,
14.1459966961117));
#177897=CARTESIAN_POINT('Ctrl Pts',(16.8549327780734,-17.9743101323951,
14.1498507172934));
#177898=CARTESIAN_POINT('Ctrl Pts',(16.9337290477334,-17.8345657051403,
14.1586405472823));
#177899=CARTESIAN_POINT('Ctrl Pts',(16.982367371586,-17.7597685692748,14.1635988425243));
#177900=CARTESIAN_POINT('Ctrl Pts',(17.0559411059934,-17.6608874095257,
14.1706897752876));
#177901=CARTESIAN_POINT('Ctrl Pts',(17.0769686667388,-17.634008975664,14.1726760492236));
#177902=CARTESIAN_POINT('Ctrl Pts',(17.1055473192068,-17.5992438041695,
14.1753299172114));
#177903=CARTESIAN_POINT('Ctrl Pts',(17.1125234962165,-17.5908896444725,
14.1759743065694));
#177904=CARTESIAN_POINT('Ctrl Pts',(17.1240365196256,-17.5773166167404,
14.1770323875731));
#177905=CARTESIAN_POINT('Ctrl Pts',(17.1285351201684,-17.5720654616132,
14.1774445069301));
#177906=CARTESIAN_POINT('Ctrl Pts',(17.1372798227453,-17.5619585320599,
14.1782431354147));
#177907=CARTESIAN_POINT('Ctrl Pts',(17.1415225553785,-17.5570999340496,
14.1786295022534));
#177908=CARTESIAN_POINT('Ctrl Pts',(17.1513511825713,-17.5459478922079,
14.1795220507335));
#177909=CARTESIAN_POINT('Ctrl Pts',(17.1569525011313,-17.5396682428503,
14.1800288754498));
#177910=CARTESIAN_POINT('Ctrl Pts',(17.1720744880781,-17.5229170811656,
14.1813923634545));
#177911=CARTESIAN_POINT('Ctrl Pts',(17.1816628467637,-17.5125075057123,
14.1822518835076));
#177912=CARTESIAN_POINT('Ctrl Pts',(17.2658129781242,-17.4229686983819,
14.1897533296712));
#177913=CARTESIAN_POINT('Ctrl Pts',(17.34625215017,-17.3496082241773,14.1966547814615));
#177914=CARTESIAN_POINT('Ctrl Pts',(17.5089830018816,-17.2226749493561,
14.210092937947));
#177915=CARTESIAN_POINT('Ctrl Pts',(17.5900728316884,-17.1679986054793,
14.2165774440231));
#177916=CARTESIAN_POINT('Ctrl Pts',(17.7368988642659,-17.0831370273213,
14.2277551380599));
#177917=CARTESIAN_POINT('Ctrl Pts',(17.8009519285969,-17.0503475038104,
14.2324604151131));
#177918=CARTESIAN_POINT('Ctrl Pts',(17.8972652897789,-17.0070841781335,
14.2391770255881));
#177919=CARTESIAN_POINT('Ctrl Pts',(17.9283038549006,-16.9940223322516,
14.241289008369));
#177920=CARTESIAN_POINT('Ctrl Pts',(17.9664235875241,-16.9790406661045,
14.2438082312705));
#177921=CARTESIAN_POINT('Ctrl Pts',(17.9732182724655,-16.9764106578555,
14.2442544266867));
#177922=CARTESIAN_POINT('Ctrl Pts',(17.9839067519935,-16.9723368057187,
14.2449517087929));
#177923=CARTESIAN_POINT('Ctrl Pts',(17.9877913733167,-16.9708692800211,
14.2452041766294));
#177924=CARTESIAN_POINT('Ctrl Pts',(17.995020427257,-16.9681625794067,14.2456722022112));
#177925=CARTESIAN_POINT('Ctrl Pts',(17.9983636408144,-16.9669204379694,
14.2458879312512));
#177926=CARTESIAN_POINT('Ctrl Pts',(18.0059506754657,-16.9641233418396,
14.2463758901694));
#177927=CARTESIAN_POINT('Ctrl Pts',(18.0101963359913,-16.9625735289155,
14.2466478116417));
#177928=CARTESIAN_POINT('Ctrl Pts',(18.0228077880583,-16.9580156290841,
14.247452256275));
#177929=CARTESIAN_POINT('Ctrl Pts',(18.0311877202684,-16.9550465855451,
14.247982513526));
#177930=CARTESIAN_POINT('Ctrl Pts',(18.0942139625286,-16.9331620151875,
14.2519403909262));
#177931=CARTESIAN_POINT('Ctrl Pts',(18.1496012505542,-16.9164380746681,
14.255248677143));
#177932=CARTESIAN_POINT('Ctrl Pts',(18.3636338700943,-16.8612707309285,
14.2676340021751));
#177933=CARTESIAN_POINT('Ctrl Pts',(18.5258439248858,-16.8389459585693,
14.2762394491432));
#177934=CARTESIAN_POINT('Ctrl Pts',(18.7490749118662,-16.8342015245125,
14.2886071776783));
#177935=CARTESIAN_POINT('Ctrl Pts',(18.8091564934396,-16.8354820255666,
14.2919822494349));
#177936=CARTESIAN_POINT('Ctrl Pts',(18.8932432274277,-16.8408590982979,
14.2968207052173));
#177937=CARTESIAN_POINT('Ctrl Pts',(18.9173581669781,-16.8428167392094,
14.2982214758417));
#177938=CARTESIAN_POINT('Ctrl Pts',(18.9594161826665,-16.8469577075536,
14.3006904980823));
#177939=CARTESIAN_POINT('Ctrl Pts',(18.977374937732,-16.8489583651079,14.3017530750738));
#177940=CARTESIAN_POINT('Ctrl Pts',(19.0037768069369,-16.8522423120571,
14.3033282949119));
#177941=CARTESIAN_POINT('Ctrl Pts',(19.01224158611,-16.8533472202056,14.3038353154866));
#177942=CARTESIAN_POINT('Ctrl Pts',(19.0270865299337,-16.8553763227179,
14.3047280687395));
#177943=CARTESIAN_POINT('Ctrl Pts',(19.0334696257948,-16.8562785251909,
14.3051131014711));
#177944=CARTESIAN_POINT('Ctrl Pts',(19.0458676187016,-16.8580886859364,
14.3058632563624));
#177945=CARTESIAN_POINT('Ctrl Pts',(19.0518829247914,-16.8589934429909,
14.306228273523));
#177946=CARTESIAN_POINT('Ctrl Pts',(19.066272109426,-16.8612211697439,14.3071039899289));
#177947=CARTESIAN_POINT('Ctrl Pts',(19.0746420552448,-16.8625685321894,
14.3076154588562));
#177948=CARTESIAN_POINT('Ctrl Pts',(19.1049271193319,-16.8676305171145,
14.3094737797347));
#177949=CARTESIAN_POINT('Ctrl Pts',(19.1267908895736,-16.8716398564208,
14.3108299491941));
#177950=CARTESIAN_POINT('Ctrl Pts',(19.3294007880085,-16.9121018499462,
14.3235376178334));
#177951=CARTESIAN_POINT('Ctrl Pts',(19.5046902285641,-16.9716727409204,
14.3356765760265));
#177952=CARTESIAN_POINT('Ctrl Pts',(19.7426185366837,-17.0889564753652,
14.3531919332245));
#177953=CARTESIAN_POINT('Ctrl Pts',(19.8131220253681,-17.1288872980212,
14.3585128420122));
#177954=CARTESIAN_POINT('Ctrl Pts',(19.911632341301,-17.1924020726889,14.3659860246247));
#177955=CARTESIAN_POINT('Ctrl Pts',(19.9415884070687,-17.2128239305798,
14.368263613347));
#177956=CARTESIAN_POINT('Ctrl Pts',(19.977076867882,-17.2383766921879,14.3709540979527));
#177957=CARTESIAN_POINT('Ctrl Pts',(19.9831234246218,-17.2427792376527,
14.3714122243153));
#177958=CARTESIAN_POINT('Ctrl Pts',(19.9924983380312,-17.2496815055131,
14.3721219252348));
#177959=CARTESIAN_POINT('Ctrl Pts',(19.9958428000915,-17.2521591039025,
14.37237498762));
#177960=CARTESIAN_POINT('Ctrl Pts',(20.0020387373891,-17.2567774559933,
14.3728435516808));
#177961=CARTESIAN_POINT('Ctrl Pts',(20.0048920845525,-17.2589155298896,
14.3730592281751));
#177962=CARTESIAN_POINT('Ctrl Pts',(20.0113396306019,-17.2637722971219,
14.3735463525865));
#177963=CARTESIAN_POINT('Ctrl Pts',(20.014930548973,-17.2664952571287,14.3738174965195));
#177964=CARTESIAN_POINT('Ctrl Pts',(20.0257640529109,-17.2747648196623,
14.3746351320544));
#177965=CARTESIAN_POINT('Ctrl Pts',(20.032979617025,-17.2803468721445,14.3751791907405));
#177966=CARTESIAN_POINT('Ctrl Pts',(20.0884681320401,-17.3238497285166,
14.3793609724962));
#177967=CARTESIAN_POINT('Ctrl Pts',(20.1351119679583,-17.3638111044263,
14.3828641416323));
#177968=CARTESIAN_POINT('Ctrl Pts',(20.2872061039383,-17.5060398419072,
14.3945010096608));
#177969=CARTESIAN_POINT('Ctrl Pts',(20.3837338277971,-17.6172218003159,
14.4022872173824));
#177970=CARTESIAN_POINT('Ctrl Pts',(20.5211938675895,-17.8134787008976,
14.4154842761584));
#177971=CARTESIAN_POINT('Ctrl Pts',(20.5693505080626,-17.8928596401075,
14.4206926499907));
#177972=CARTESIAN_POINT('Ctrl Pts',(20.6218690755522,-17.9938332639764,
14.4273222592249));
#177973=CARTESIAN_POINT('Ctrl Pts',(20.6313137059699,-18.0126737551051,
14.4285591331837));
#177974=CARTESIAN_POINT('Ctrl Pts',(20.6443687957487,-18.0397169988001,
14.430335654894));
#177975=CARTESIAN_POINT('Ctrl Pts',(20.6482110792106,-18.0478069063957,
14.4308672368226));
#177976=CARTESIAN_POINT('Ctrl Pts',(20.6547602422308,-18.061824983953,14.4317886996085));
#177977=CARTESIAN_POINT('Ctrl Pts',(20.6574913145826,-18.0677417636292,
14.4321777378722));
#177978=CARTESIAN_POINT('Ctrl Pts',(20.6626744817152,-18.0791085643564,
14.4329253651094));
#177979=CARTESIAN_POINT('Ctrl Pts',(20.665130906204,-18.0845565512354,14.4332838003344));
#177980=CARTESIAN_POINT('Ctrl Pts',(20.6714720453677,-18.0987806934464,
14.4342199500857));
#177981=CARTESIAN_POINT('Ctrl Pts',(20.6753201734384,-18.1075729213761,
14.4347989114098));
#177982=CARTESIAN_POINT('Ctrl Pts',(20.6883060613078,-18.1378011210538,
14.4367906461468));
#177983=CARTESIAN_POINT('Ctrl Pts',(20.6971493581847,-18.1593610373518,
14.4382133627017));
#177984=CARTESIAN_POINT('Ctrl Pts',(20.7678865584375,-18.3402677991235,
14.4501731097673));
#177985=CARTESIAN_POINT('Ctrl Pts',(20.8106148009925,-18.506399219495,14.4613733882527));
#177986=CARTESIAN_POINT('Ctrl Pts',(20.8446793196122,-18.7652813297502,
14.4786282131894));
#177987=CARTESIAN_POINT('Ctrl Pts',(20.8507199765435,-18.8554102135709,
14.4845832112794));
#177988=CARTESIAN_POINT('Ctrl Pts',(20.8511062741943,-18.9842805476592,
14.492816667076));
#177989=CARTESIAN_POINT('Ctrl Pts',(20.8501648843296,-19.0229057614886,
14.49524767335));
#177990=CARTESIAN_POINT('Ctrl Pts',(20.8477729847385,-19.0690930749978,
14.4980939188358));
#177991=CARTESIAN_POINT('Ctrl Pts',(20.8473379911583,-19.0766978684573,
14.4985605793421));
#177992=CARTESIAN_POINT('Ctrl Pts',(20.8465999734401,-19.0884841591562,
14.4992805940618));
#177993=CARTESIAN_POINT('Ctrl Pts',(20.8463255636522,-19.0926672930147,
14.499535505224));
#177994=CARTESIAN_POINT('Ctrl Pts',(20.8457949436417,-19.1004042133233,
14.5000057705053));
#177995=CARTESIAN_POINT('Ctrl Pts',(20.8455421897163,-19.1039581385761,
14.5002213103369));
#177996=CARTESIAN_POINT('Ctrl Pts',(20.844952295327,-19.111966758852,14.5007059614379));
#177997=CARTESIAN_POINT('Ctrl Pts',(20.8446100268816,-19.1164210216253,
14.5009747819627));
#177998=CARTESIAN_POINT('Ctrl Pts',(20.8435639095311,-19.1294933131671,
14.501761642187));
#177999=CARTESIAN_POINT('Ctrl Pts',(20.842821348907,-19.1381082717019,14.5022775606373));
#178000=CARTESIAN_POINT('Ctrl Pts',(20.837275220557,-19.1981507254997,14.5058563523392));
#178001=CARTESIAN_POINT('Ctrl Pts',(20.830643309437,-19.2493963689155,14.5088242487981));
#178002=CARTESIAN_POINT('Ctrl Pts',(20.8185587282442,-19.3218354773013,
14.5129602891302));
#178003=CARTESIAN_POINT('Ctrl Pts',(20.8146434089476,-19.3432625994992,
14.5141762367099));
#178004=CARTESIAN_POINT('Ctrl Pts',(20.8014003700517,-19.409903629592,14.5179447994881));
#178005=CARTESIAN_POINT('Ctrl Pts',(20.7909238627403,-19.45487621983,14.5204691498698));
#178006=CARTESIAN_POINT('Ctrl Pts',(20.7507051162463,-19.6051064020344,
14.5289363649793));
#178007=CARTESIAN_POINT('Ctrl Pts',(20.7142828981661,-19.7083902818046,
14.5348247068131));
#178008=CARTESIAN_POINT('Ctrl Pts',(20.6477506739108,-19.8587994047399,
14.5439696281747));
#178009=CARTESIAN_POINT('Ctrl Pts',(20.623495817134,-19.9083115150446,14.5470774800121));
#178010=CARTESIAN_POINT('Ctrl Pts',(20.5810528673916,-19.9870178315409,
14.5522219968268));
#178011=CARTESIAN_POINT('Ctrl Pts',(20.5640366493465,-20.0168154168468,
14.554219263986));
#178012=CARTESIAN_POINT('Ctrl Pts',(20.5407177316318,-20.0554386606359,
14.5568800886423));
#178013=CARTESIAN_POINT('Ctrl Pts',(20.5350601990483,-20.0646490877286,
14.557520113803));
#178014=CARTESIAN_POINT('Ctrl Pts',(20.5256770207777,-20.0796657479039,
14.558572843665));
#178015=CARTESIAN_POINT('Ctrl Pts',(20.5219930462509,-20.0854978829294,
14.5589840069489));
#178016=CARTESIAN_POINT('Ctrl Pts',(20.514805789859,-20.0967538727245,14.5597820776845));
#178017=CARTESIAN_POINT('Ctrl Pts',(20.5113060650999,-20.1021799162912,
14.5601688497291));
#178018=CARTESIAN_POINT('Ctrl Pts',(20.5031665841764,-20.1146736759997,
14.5610642169183));
#178019=CARTESIAN_POINT('Ctrl Pts',(20.4985092254094,-20.1217297421348,
14.5615734681397));
#178020=CARTESIAN_POINT('Ctrl Pts',(20.4858668763241,-20.140636039178,14.5629477350517));
#178021=CARTESIAN_POINT('Ctrl Pts',(20.4778040714258,-20.1524334761901,
14.5638156785344));
#178022=CARTESIAN_POINT('Ctrl Pts',(20.4027425002855,-20.2599108981909,
14.5718202652279));
#178023=CARTESIAN_POINT('Ctrl Pts',(20.3280628686515,-20.3499585909559,
14.5792584515377));
#178024=CARTESIAN_POINT('Ctrl Pts',(20.132580043701,-20.5495285974901,14.5975057692211));
#178025=CARTESIAN_POINT('Ctrl Pts',(20.0058105119725,-20.6521828818894,
14.6084546158184));
#178026=CARTESIAN_POINT('Ctrl Pts',(19.840960588158,-20.7568253574901,14.620863600959));
#178027=CARTESIAN_POINT('Ctrl Pts',(19.8129751083141,-20.7736940749651,
14.6229114294141));
#178028=CARTESIAN_POINT('Ctrl Pts',(19.7783138859935,-20.793507556201,14.6253665621806));
#178029=CARTESIAN_POINT('Ctrl Pts',(19.7720005560008,-20.7970735544335,
14.6258105193929));
#178030=CARTESIAN_POINT('Ctrl Pts',(19.7620781585256,-20.8026110367418,
14.6265030697708));
#178031=CARTESIAN_POINT('Ctrl Pts',(19.7584815253384,-20.804604521816,14.6267530389589));
#178032=CARTESIAN_POINT('Ctrl Pts',(19.7517502413733,-20.8083098346129,
14.6272188513599));
#178033=CARTESIAN_POINT('Ctrl Pts',(19.7486171014945,-20.8100241907691,
14.6274348509351));
#178034=CARTESIAN_POINT('Ctrl Pts',(19.7414581823612,-20.8139178193558,
14.6279265434622));
#178035=CARTESIAN_POINT('Ctrl Pts',(19.7374296717057,-20.8160919639559,
14.6282019084627));
#178036=CARTESIAN_POINT('Ctrl Pts',(19.7250361554935,-20.8227287954197,
14.6290450966787));
#178037=CARTESIAN_POINT('Ctrl Pts',(19.7166480653741,-20.8271484407077,
14.6296102577913));
#178038=CARTESIAN_POINT('Ctrl Pts',(19.6008140007761,-20.8871901352769,
14.6373429775697));
#178039=CARTESIAN_POINT('Ctrl Pts',(19.4888054128516,-20.9335662313437,
14.6439804893635));
#178040=CARTESIAN_POINT('Ctrl Pts',(19.2028073969266,-21.0241835424842,
14.6603064431349));
#178041=CARTESIAN_POINT('Ctrl Pts',(19.0260361519297,-21.0563842011585,
14.6699251200044));
#178042=CARTESIAN_POINT('Ctrl Pts',(18.8258763563366,-21.067114455345,14.6815960702804));
#178043=CARTESIAN_POINT('Ctrl Pts',(18.8044107241675,-21.0679377835882,
14.6828564248385));
#178044=CARTESIAN_POINT('Ctrl Pts',(18.7739144021392,-21.0686429289018,
14.684660813919));
#178045=CARTESIAN_POINT('Ctrl Pts',(18.7648908277235,-21.0687938494076,
14.6851964272703));
#178046=CARTESIAN_POINT('Ctrl Pts',(18.7493378521133,-21.0689545059572,
14.6861226616634));
#178047=CARTESIAN_POINT('Ctrl Pts',(18.7428088152758,-21.0689917414342,
14.6865124162515));
#178048=CARTESIAN_POINT('Ctrl Pts',(18.7303180253181,-21.0690051925921,
14.6872598749605));
#178049=CARTESIAN_POINT('Ctrl Pts',(18.7243563316378,-21.068986429085,14.6876174178959));
#178050=CARTESIAN_POINT('Ctrl Pts',(18.7088771923154,-21.0688723237703,
14.6885478437945));
#178051=CARTESIAN_POINT('Ctrl Pts',(18.6993602465184,-21.0687379794065,
14.6891219436901));
#178052=CARTESIAN_POINT('Ctrl Pts',(18.6670303135176,-21.0680635107621,
14.6910793565644));
#178053=CARTESIAN_POINT('Ctrl Pts',(18.6442259007042,-21.0672187280819,
14.6924721559598));
#178054=CARTESIAN_POINT('Ctrl Pts',(18.4439242820799,-21.0565537158359,
14.7048164569888));
#178055=CARTESIAN_POINT('Ctrl Pts',(18.2683373930392,-21.0247817708654,
14.7164925038476));
#178056=CARTESIAN_POINT('Ctrl Pts',(18.0173335129665,-20.9458345030525,
14.7338754485258));
#178057=CARTESIAN_POINT('Ctrl Pts',(17.9374624474419,-20.9152923066633,
14.739501754004));
#178058=CARTESIAN_POINT('Ctrl Pts',(17.8255729443369,-20.8645505134323,
14.74734295224));
#178059=CARTESIAN_POINT('Ctrl Pts',(17.7919077579063,-20.8481940268046,
14.7496960751315));
#178060=CARTESIAN_POINT('Ctrl Pts',(17.751991916602,-20.8274749010043,14.7524633792915));
#178061=CARTESIAN_POINT('Ctrl Pts',(17.7453107263114,-20.8239614056363,
14.7529257930619));
#178062=CARTESIAN_POINT('Ctrl Pts',(17.7349616584056,-20.8184481886917,
14.7536406770263));
#178063=CARTESIAN_POINT('Ctrl Pts',(17.7312807435791,-20.8164732614186,
14.7538946696059));
#178064=CARTESIAN_POINT('Ctrl Pts',(17.7244699982195,-20.8127930778915,
14.7543640846775));
#178065=CARTESIAN_POINT('Ctrl Pts',(17.7213386562089,-20.8110908278804,
14.7545796874812));
#178066=CARTESIAN_POINT('Ctrl Pts',(17.7142752508495,-20.8072279010215,
14.7550655450462));
#178067=CARTESIAN_POINT('Ctrl Pts',(17.710345759237,-20.805062633852,14.7553355025786));
#178068=CARTESIAN_POINT('Ctrl Pts',(17.6987856735437,-20.7986446892405,
14.756128789491));
#178069=CARTESIAN_POINT('Ctrl Pts',(17.6911743769557,-20.7943571955166,
14.7566499452989));
#178070=CARTESIAN_POINT('Ctrl Pts',(17.6369037680884,-20.7633421219217,
14.7603592304453));
#178071=CARTESIAN_POINT('Ctrl Pts',(17.5912470088454,-20.7348900885347,
14.763444330768));
#178072=CARTESIAN_POINT('Ctrl Pts',(17.4071720841302,-20.6101995480509,
14.7759434078619));
#178073=CARTESIAN_POINT('Ctrl Pts',(17.2794066333268,-20.4993409289175,
14.7848132778786));
#178074=CARTESIAN_POINT('Ctrl Pts',(17.1115465626614,-20.3143267011366,
14.7986576589763));
#178075=CARTESIAN_POINT('Ctrl Pts',(17.060471157986,-20.2510721018573,14.803248767792));
#178076=CARTESIAN_POINT('Ctrl Pts',(17.0017259930104,-20.169087141203,14.8091326216188));
#178077=CARTESIAN_POINT('Ctrl Pts',(16.9905152035284,-20.1529725520273,
14.8102859077259));
#178078=CARTESIAN_POINT('Ctrl Pts',(16.9746597467292,-20.1294916668556,
14.8119628559975));
#178079=CARTESIAN_POINT('Ctrl Pts',(16.9698336794635,-20.1222486668776,
14.8124796554925));
#178080=CARTESIAN_POINT('Ctrl Pts',(16.9614964409842,-20.1095672917066,
14.8133837561062));
#178081=CARTESIAN_POINT('Ctrl Pts',(16.957965271981,-20.1041421548521,14.813770301005));
#178082=CARTESIAN_POINT('Ctrl Pts',(16.9511894776933,-20.0936269431713,
14.81451910815));
#178083=CARTESIAN_POINT('Ctrl Pts',(16.9479416283479,-20.0885390128369,
14.8148812452003));
#178084=CARTESIAN_POINT('Ctrl Pts',(16.9402801644432,-20.0764229744615,
14.815743212904));
#178085=CARTESIAN_POINT('Ctrl Pts',(16.9358860544753,-20.0693827051681,
14.816243759427));
#178086=CARTESIAN_POINT('Ctrl Pts',(16.9204544008849,-20.0443312629719,
14.8180238565611));
#178087=CARTESIAN_POINT('Ctrl Pts',(16.9096454486403,-20.026181385203,14.8193117372901));
#178088=CARTESIAN_POINT('Ctrl Pts',(16.8022349832156,-19.8395241725488,
14.8325423885839));
#178089=CARTESIAN_POINT('Ctrl Pts',(16.7290069376686,-19.6586727857104,
14.8453728731502));
#178090=CARTESIAN_POINT('Ctrl Pts',(16.6631797526465,-19.398055295425,14.8631017321562));
#178091=CARTESIAN_POINT('Ctrl Pts',(16.6487382168833,-19.3247554843099,
14.8679934972455));
#178092=CARTESIAN_POINT('Ctrl Pts',(16.6333272062598,-19.2166767412335,
14.8749433504138));
#178093=CARTESIAN_POINT('Ctrl Pts',(16.6292914350924,-19.1823956121774,
14.8771093014166));
#178094=CARTESIAN_POINT('Ctrl Pts',(16.6254128237801,-19.1406888023454,
14.8796857585881));
#178095=CARTESIAN_POINT('Ctrl Pts',(16.6247685436926,-19.1333450061363,
14.8801372228181));
#178096=CARTESIAN_POINT('Ctrl Pts',(16.623822466253,-19.1218732017602,14.8808388637963));
#178097=CARTESIAN_POINT('Ctrl Pts',(16.6234943983514,-19.1177475028299,
14.8810904753447));
#178098=CARTESIAN_POINT('Ctrl Pts',(16.622906023878,-19.1100631372184,14.881557733176));
#178099=CARTESIAN_POINT('Ctrl Pts',(16.6226426178642,-19.106504810681,14.8817735456592));
#178100=CARTESIAN_POINT('Ctrl Pts',(16.6220645668639,-19.098418333969,14.8822627418272));
#178101=CARTESIAN_POINT('Ctrl Pts',(16.6217554883487,-19.093889838036,14.8825358105878));
#178102=CARTESIAN_POINT('Ctrl Pts',(16.6209918952332,-19.0821461257066,
14.8832417434411));
#178103=CARTESIAN_POINT('Ctrl Pts',(16.6205597666391,-19.0749294441844,
14.883673383521));
#178104=CARTESIAN_POINT('Ctrl Pts',(16.6180743366898,-19.029524866141,14.8863762676856));
#178105=CARTESIAN_POINT('Ctrl Pts',(16.6170190193761,-18.9912868187921,
14.8885955085252));
#178106=CARTESIAN_POINT('Ctrl Pts',(16.6169207098347,-18.7909008080633,
14.9000236618683));
#178107=CARTESIAN_POINT('Ctrl Pts',(16.6354677289579,-18.629276688061,14.9085853047104));
#178108=CARTESIAN_POINT('Ctrl Pts',(16.6916958548057,-18.3880942781729,
14.9221735828745));
#178109=CARTESIAN_POINT('Ctrl Pts',(16.7161208887108,-18.3061287994777,
14.926935560901));
#178110=CARTESIAN_POINT('Ctrl Pts',(16.7454193926287,-18.2258896998479,
14.9318514575852));
#178111=CARTESIAN_POINT('Origin',(18.734,-18.952,0.));
#178112=CARTESIAN_POINT('',(16.7454193691905,-18.2258897640378,15.9575278689401));
#178113=CARTESIAN_POINT('',(16.7454193749215,-18.2258897483422,15.7328935260819));
#178114=CARTESIAN_POINT('',(16.7454193692319,-18.2258897639242,0.));
#178115=CARTESIAN_POINT('',(16.6170004656572,-18.9534041339617,15.9109437209775));
#178116=CARTESIAN_POINT('Ctrl Pts',(16.7454193691904,-18.2258897640378,
15.9575278689401));
#178117=CARTESIAN_POINT('Ctrl Pts',(16.7400018536359,-18.240726583525,15.9565689505998));
#178118=CARTESIAN_POINT('Ctrl Pts',(16.7347506147815,-18.2556234021838,
15.9556045111451));
#178119=CARTESIAN_POINT('Ctrl Pts',(16.6996529154685,-18.3588596237815,
15.9489084765267));
#178120=CARTESIAN_POINT('Ctrl Pts',(16.6755084838295,-18.449016641622,15.9429915915783));
#178121=CARTESIAN_POINT('Ctrl Pts',(16.6304385517586,-18.6764384866331,
15.92794103383));
#178122=CARTESIAN_POINT('Ctrl Pts',(16.6169140929087,-18.8147188280224,
15.9186647458253));
#178123=CARTESIAN_POINT('Ctrl Pts',(16.6170004105498,-18.9533184338415,
15.9096291502085));
#178124=CARTESIAN_POINT('Ctrl Pts',(16.7454193692319,-18.2258897639242,
15.1555945373748));
#178125=CARTESIAN_POINT('Ctrl Pts',(16.7703664756571,-18.1575677238728,
15.1599719862091));
#178126=CARTESIAN_POINT('Ctrl Pts',(16.7988694213885,-18.0904486586419,
15.1643494350433));
#178127=CARTESIAN_POINT('Ctrl Pts',(16.8307867059135,-18.0249249452108,
15.1687268838775));
#178128=CARTESIAN_POINT('Ctrl Pts',(16.8626811668449,-17.95944808685,15.1731012024607));
#178129=CARTESIAN_POINT('Ctrl Pts',(16.897984912061,-17.89556474928,15.1774755210439));
#178130=CARTESIAN_POINT('Ctrl Pts',(16.9365084077469,-17.8336472042422,
15.1818498396271));
#178131=CARTESIAN_POINT('Ctrl Pts',(16.9750170641353,-17.771753509918,15.1862224732175));
#178132=CARTESIAN_POINT('Ctrl Pts',(17.0167427546477,-17.7118245143087,
15.1905951068078));
#178133=CARTESIAN_POINT('Ctrl Pts',(17.061450917826,-17.6542062691942,15.1949677403982));
#178134=CARTESIAN_POINT('Ctrl Pts',(17.1061566074958,-17.596591211847,15.1993401320697));
#178135=CARTESIAN_POINT('Ctrl Pts',(17.1538441452889,-17.5412870313143,
15.2037125237412));
#178136=CARTESIAN_POINT('Ctrl Pts',(17.2042377414628,-17.4886079020457,
15.2080849154128));
#178137=CARTESIAN_POINT('Ctrl Pts',(17.254681022044,-17.435876835001,15.2124616179433));
#178138=CARTESIAN_POINT('Ctrl Pts',(17.3078353564725,-17.3857763388251,
15.2168383204739));
#178139=CARTESIAN_POINT('Ctrl Pts',(17.3633875710639,-17.3385841919562,
15.2212150230044));
#178140=CARTESIAN_POINT('Ctrl Pts',(17.4189660949095,-17.2913696951198,
15.2255937983196));
#178141=CARTESIAN_POINT('Ctrl Pts',(17.476944377479,-17.2470665850251,15.2299725736349));
#178142=CARTESIAN_POINT('Ctrl Pts',(17.5369777562186,-17.2059110137532,
15.2343513489501));
#178143=CARTESIAN_POINT('Ctrl Pts',(17.5971223014476,-17.1646792328712,
15.2387382326392));
#178144=CARTESIAN_POINT('Ctrl Pts',(17.6593291342759,-17.126606889442,15.2431251163283));
#178145=CARTESIAN_POINT('Ctrl Pts',(17.7232266804942,-17.0918854076764,
15.2475120000174));
#178146=CARTESIAN_POINT('Ctrl Pts',(17.7823156149067,-17.0597768920889,
15.2515687486396));
#178147=CARTESIAN_POINT('Ctrl Pts',(17.8428498273126,-17.030533487829,15.2556254972618));
#178148=CARTESIAN_POINT('Ctrl Pts',(17.9045214391032,-17.0042694444527,
15.2596822458839));
#178149=CARTESIAN_POINT('Ctrl Pts',(17.9712319856141,-16.9758594737004,
15.2640704548148));
#178150=CARTESIAN_POINT('Ctrl Pts',(18.0395340178847,-16.9508253061037,
15.2684586637457));
#178151=CARTESIAN_POINT('Ctrl Pts',(18.1090523123262,-16.9293459545263,
15.2728468726766));
#178152=CARTESIAN_POINT('Ctrl Pts',(18.1784674300925,-16.9078984818679,
15.2772285687779));
#178153=CARTESIAN_POINT('Ctrl Pts',(18.2490947695204,-16.8899954929979,
15.2816102648792));
#178154=CARTESIAN_POINT('Ctrl Pts',(18.3205388114184,-16.8757681137367,
15.2859919609805));
#178155=CARTESIAN_POINT('Ctrl Pts',(18.3918989008814,-16.8615574527783,
15.2903685082401));
#178156=CARTESIAN_POINT('Ctrl Pts',(18.464073315643,-16.8510139151847,15.2947450554998));
#178157=CARTESIAN_POINT('Ctrl Pts',(18.5366526876881,-16.84421845574,15.2991216027594));
#178158=CARTESIAN_POINT('Ctrl Pts',(18.6091860309502,-16.8374273058768,
15.3034953744764));
#178159=CARTESIAN_POINT('Ctrl Pts',(18.6821233428399,-16.8343795627893,
15.3078691461934));
#178160=CARTESIAN_POINT('Ctrl Pts',(18.7550478100786,-16.8351046342129,
15.3122429179104));
#178161=CARTESIAN_POINT('Ctrl Pts',(18.8279500861569,-16.8358294849948,
15.3166153586739));
#178162=CARTESIAN_POINT('Ctrl Pts',(18.9008390432801,-16.840324866202,15.3209877994375));
#178163=CARTESIAN_POINT('Ctrl Pts',(18.973297213937,-16.8485680796845,15.3253602402011));
#178164=CARTESIAN_POINT('Ctrl Pts',(19.0457572373573,-16.856811503947,15.3297327927684));
#178165=CARTESIAN_POINT('Ctrl Pts',(19.1177859733816,-16.8688028942383,
15.3341053453358));
#178166=CARTESIAN_POINT('Ctrl Pts',(19.1889721056856,-16.8844678036248,
15.3384778979031));
#178167=CARTESIAN_POINT('Ctrl Pts',(19.2602321176428,-16.9001489706452,
15.3428549884705));
#178168=CARTESIAN_POINT('Ctrl Pts',(19.3306473077957,-16.9195111648159,
15.3472320790378));
#178169=CARTESIAN_POINT('Ctrl Pts',(19.3998183959356,-16.9424291842202,
15.3516091696051));
#178170=CARTESIAN_POINT('Ctrl Pts',(19.469027260974,-16.9653597200056,15.3559886506641));
#178171=CARTESIAN_POINT('Ctrl Pts',(19.5369902214648,-16.9918497721618,
15.360368131723));
#178172=CARTESIAN_POINT('Ctrl Pts',(19.6033275197911,-17.0217257543722,
15.364747612782));
#178173=CARTESIAN_POINT('Ctrl Pts',(19.6697824005334,-17.0516546915606,
15.3691348564417));
#178174=CARTESIAN_POINT('Ctrl Pts',(19.7346054355421,-17.0849813228797,
15.3735221001015));
#178175=CARTESIAN_POINT('Ctrl Pts',(19.7974415556907,-17.1214861219783,
15.3779093437612));
#178176=CARTESIAN_POINT('Ctrl Pts',(19.8401640625164,-17.1463058677706,
15.3808922466959));
#178177=CARTESIAN_POINT('Ctrl Pts',(19.8819686426658,-17.1725938434287,
15.3838751496307));
#178178=CARTESIAN_POINT('Ctrl Pts',(19.9227521494642,-17.2002701900281,
15.3868580525654));
#178179=CARTESIAN_POINT('Ctrl Pts',(19.9827495924521,-17.2409854241402,
15.3912462614963));
#178180=CARTESIAN_POINT('Ctrl Pts',(20.0407699602753,-17.2848661041391,
15.3956344704272));
#178181=CARTESIAN_POINT('Ctrl Pts',(20.0964596300331,-17.3316936226349,
15.4000226793581));
#178182=CARTESIAN_POINT('Ctrl Pts',(20.1520666470875,-17.3784516413291,
15.4044043754594));
#178183=CARTESIAN_POINT('Ctrl Pts',(20.2053494667964,-17.4281475084506,
15.4087860715606));
#178184=CARTESIAN_POINT('Ctrl Pts',(20.2559837460593,-17.4805196308713,
15.4131677676619));
#178185=CARTESIAN_POINT('Ctrl Pts',(20.3065585260145,-17.5328302118802,
15.4175443149215));
#178186=CARTESIAN_POINT('Ctrl Pts',(20.354490614394,-17.5878104559203,15.4219208621811));
#178187=CARTESIAN_POINT('Ctrl Pts',(20.3994903578935,-17.6451599685639,
15.4262974094408));
#178188=CARTESIAN_POINT('Ctrl Pts',(20.4444615632096,-17.7024731109801,
15.4306711811577));
#178189=CARTESIAN_POINT('Ctrl Pts',(20.4865038163907,-17.7621521621709,
15.4350449528747));
#178190=CARTESIAN_POINT('Ctrl Pts',(20.5253667770628,-17.8238625659807,
15.4394187245917));
#178191=CARTESIAN_POINT('Ctrl Pts',(20.5642179116054,-17.8855541911073,
15.4437911653552));
#178192=CARTESIAN_POINT('Ctrl Pts',(20.599891417462,-17.9492755337059,15.4481636061188));
#178193=CARTESIAN_POINT('Ctrl Pts',(20.6321804129387,-18.0146632835871,
15.4525360468823));
#178194=CARTESIAN_POINT('Ctrl Pts',(20.6644702340486,-18.0800527054402,
15.4569085994496));
#178195=CARTESIAN_POINT('Ctrl Pts',(20.6933751611692,-18.1471081857717,
15.461281152017));
#178196=CARTESIAN_POINT('Ctrl Pts',(20.7187351546652,-18.2154435759318,
15.4656537045843));
#178197=CARTESIAN_POINT('Ctrl Pts',(20.744121467719,-18.2838498871373,15.4700307951516));
#178198=CARTESIAN_POINT('Ctrl Pts',(20.7659553334552,-18.3535383070817,
15.4744078857189));
#178199=CARTESIAN_POINT('Ctrl Pts',(20.7841259040682,-18.4241053348739,
15.4787849762863));
#178200=CARTESIAN_POINT('Ctrl Pts',(20.8023063983042,-18.4947109019391,
15.4831644573452));
#178201=CARTESIAN_POINT('Ctrl Pts',(20.8168195180768,-18.5661955591485,
15.4875439384041));
#178202=CARTESIAN_POINT('Ctrl Pts',(20.8276056664123,-18.6381460314631,
15.4919234194631));
#178203=CARTESIAN_POINT('Ctrl Pts',(20.8384109331234,-18.710224035507,15.4963106631228));
#178204=CARTESIAN_POINT('Ctrl Pts',(20.8454759896221,-18.7827690229248,
15.5006979067825));
#178205=CARTESIAN_POINT('Ctrl Pts',(20.8487932306453,-18.8553636113216,
15.5050851504422));
#178206=CARTESIAN_POINT('Ctrl Pts',(20.8510486348925,-18.9047209362348,
15.5080680533771));
#178207=CARTESIAN_POINT('Ctrl Pts',(20.8515726338748,-18.9541011550575,
15.511050956312));
#178208=CARTESIAN_POINT('Ctrl Pts',(20.8503765449711,-19.0033743116382,
15.5140338592469));
#178209=CARTESIAN_POINT('Ctrl Pts',(20.8486169543561,-19.0758610503894,
15.5184220681777));
#178210=CARTESIAN_POINT('Ctrl Pts',(20.8431255714046,-19.148398777627,15.5228102771086));
#178211=CARTESIAN_POINT('Ctrl Pts',(20.8338948009669,-19.2205718244197,
15.5271984860395));
#178212=CARTESIAN_POINT('Ctrl Pts',(20.824677730523,-19.2926377544445,15.5315801821408));
#178213=CARTESIAN_POINT('Ctrl Pts',(20.8117323505351,-19.364339603947,15.5359618782421));
#178214=CARTESIAN_POINT('Ctrl Pts',(20.7951030586573,-19.4352630563093,
15.5403435743433));
#178215=CARTESIAN_POINT('Ctrl Pts',(20.7784933075209,-19.5061031679707,
15.544720121603));
#178216=CARTESIAN_POINT('Ctrl Pts',(20.7582083534313,-19.5761662321966,
15.5490966688626));
#178217=CARTESIAN_POINT('Ctrl Pts',(20.7343439967237,-19.6450460985904,
15.5534732161222));
#178218=CARTESIAN_POINT('Ctrl Pts',(20.7104947744443,-19.713882282374,15.5578469878392));
#178219=CARTESIAN_POINT('Ctrl Pts',(20.6830708110599,-19.7815363024755,
15.5622207595562));
#178220=CARTESIAN_POINT('Ctrl Pts',(20.6522179108565,-19.8476165733558,
15.5665945312731));
#178221=CARTESIAN_POINT('Ctrl Pts',(20.6213743992941,-19.9136767357877,
15.5709669720367));
#178222=CARTESIAN_POINT('Ctrl Pts',(20.5871042264084,-19.9781636629362,
15.5753394128002));
#178223=CARTESIAN_POINT('Ctrl Pts',(20.5496008974363,-20.0407067471218,
15.5797118535638));
#178224=CARTESIAN_POINT('Ctrl Pts',(20.5120966094999,-20.1032514305409,
15.5840844061311));
#178225=CARTESIAN_POINT('Ctrl Pts',(20.471359251126,-20.1638517596412,15.5884569586985));
#178226=CARTESIAN_POINT('Ctrl Pts',(20.4276268858003,-20.2221641514759,
15.5928295112658));
#178227=CARTESIAN_POINT('Ctrl Pts',(20.3838491333763,-20.2805370621104,
15.5972066018331));
#178228=CARTESIAN_POINT('Ctrl Pts',(20.3370704580455,-20.3366169078809,
15.6015836924004));
#178229=CARTESIAN_POINT('Ctrl Pts',(20.287570140387,-20.3900920759457,15.6059607829678));
#178230=CARTESIAN_POINT('Ctrl Pts',(20.2380427887679,-20.4435964487845,
15.6103402640267));
#178231=CARTESIAN_POINT('Ctrl Pts',(20.1857911812168,-20.494492974896,15.6147197450856));
#178232=CARTESIAN_POINT('Ctrl Pts',(20.1311305579277,-20.5425078447165,
15.6190992261446));
#178233=CARTESIAN_POINT('Ctrl Pts',(20.0763730490507,-20.5906078205715,
15.6234864698043));
#178234=CARTESIAN_POINT('Ctrl Pts',(20.0191983762087,-20.6358156407823,
15.627873713464));
#178235=CARTESIAN_POINT('Ctrl Pts',(19.959953375359,-20.6778989893519,15.6322609571237));
#178236=CARTESIAN_POINT('Ctrl Pts',(19.9196724836153,-20.7065116112378,
15.6352438600586));
#178237=CARTESIAN_POINT('Ctrl Pts',(19.8784351648856,-20.7336807873357,
15.6382267629934));
#178238=CARTESIAN_POINT('Ctrl Pts',(19.8363568176097,-20.7593456909704,
15.6412096659283));
#178239=CARTESIAN_POINT('Ctrl Pts',(19.7744545085683,-20.7971018505909,
15.6455978748592));
#178240=CARTESIAN_POINT('Ctrl Pts',(19.7104893778662,-20.8317477625258,
15.6499860837901));
#178241=CARTESIAN_POINT('Ctrl Pts',(19.644806826183,-20.8630520467477,15.654374292721));
#178242=CARTESIAN_POINT('Ctrl Pts',(19.579221758297,-20.8943098702214,15.6587559888223));
#178243=CARTESIAN_POINT('Ctrl Pts',(19.5119247612699,-20.9222357055049,
15.6631376849236));
#178244=CARTESIAN_POINT('Ctrl Pts',(19.4432882414188,-20.9466426222722,
15.6675193810248));
#178245=CARTESIAN_POINT('Ctrl Pts',(19.3747323749407,-20.97102085897,15.6718959282845));
#178246=CARTESIAN_POINT('Ctrl Pts',(19.3048405647327,-20.9918882305585,
15.6762724755441));
#178247=CARTESIAN_POINT('Ctrl Pts',(19.234006173908,-21.0091054484527,15.6806490228038));
#178248=CARTESIAN_POINT('Ctrl Pts',(19.1632167052245,-21.0263117474376,
15.6850227945208));
#178249=CARTESIAN_POINT('Ctrl Pts',(19.0914863095564,-21.0398723720885,
15.6893965662378));
#178250=CARTESIAN_POINT('Ctrl Pts',(19.0192231694669,-21.0496979629106,
15.6937703379548));
#178251=CARTESIAN_POINT('Ctrl Pts',(18.9469820192935,-21.0595205637724,
15.6981427787183));
#178252=CARTESIAN_POINT('Ctrl Pts',(18.8742089242411,-21.0656103223221,
15.7025152194819));
#178253=CARTESIAN_POINT('Ctrl Pts',(18.8013202474328,-21.0679293429332,
15.7068876602454));
#178254=CARTESIAN_POINT('Ctrl Pts',(18.728429706853,-21.0702484228418,15.7112602128128));
#178255=CARTESIAN_POINT('Ctrl Pts',(18.6554240608469,-21.0687965600418,
15.7156327653801));
#178256=CARTESIAN_POINT('Ctrl Pts',(18.582721067549,-21.0635879533177,15.7200053179475));
#178257=CARTESIAN_POINT('Ctrl Pts',(18.5099426203423,-21.0583739409051,
15.7243824085148));
#178258=CARTESIAN_POINT('Ctrl Pts',(18.4374679351483,-21.0493954347148,
15.7287594990822));
#178259=CARTESIAN_POINT('Ctrl Pts',(18.3657101983337,-21.0367185953957,
15.7331365896495));
#178260=CARTESIAN_POINT('Ctrl Pts',(18.2939132719558,-21.0240348327841,
15.7375160707085));
#178261=CARTESIAN_POINT('Ctrl Pts',(18.2228345439085,-21.0076488240848,
15.7418955517674));
#178262=CARTESIAN_POINT('Ctrl Pts',(18.1528748782415,-20.9876774284894,
15.7462750328264));
#178263=CARTESIAN_POINT('Ctrl Pts',(18.0827912095367,-20.9676706337294,
15.7506622764861));
#178264=CARTESIAN_POINT('Ctrl Pts',(18.0138310210261,-20.9440659176032,
15.7550495201458));
#178265=CARTESIAN_POINT('Ctrl Pts',(17.9463773894235,-20.9170291660199,
15.7594367638056));
#178266=CARTESIAN_POINT('Ctrl Pts',(17.9005154197516,-20.8986467801989,
15.7624196667403));
#178267=CARTESIAN_POINT('Ctrl Pts',(17.8553494637696,-20.8786788808127,
15.765402569675));
#178268=CARTESIAN_POINT('Ctrl Pts',(17.8109931300721,-20.8571895753615,
15.7683854726098));
#178269=CARTESIAN_POINT('Ctrl Pts',(17.7457396290593,-20.8255762228108,
15.7727736815407));
#178270=CARTESIAN_POINT('Ctrl Pts',(17.6819847879021,-20.7905448456105,
15.7771618904716));
#178271=CARTESIAN_POINT('Ctrl Pts',(17.6201101194241,-20.7522606294508,
15.7815500994025));
#178272=CARTESIAN_POINT('Ctrl Pts',(17.558327283213,-20.7140332334155,15.7859317955037));
#178273=CARTESIAN_POINT('Ctrl Pts',(17.4984194869967,-20.6725628338802,
15.790313491605));
#178274=CARTESIAN_POINT('Ctrl Pts',(17.4407454860729,-20.6280613837826,
15.7946951877063));
#178275=CARTESIAN_POINT('Ctrl Pts',(17.38313925669,-20.5836122264304,15.7990717349659));
#178276=CARTESIAN_POINT('Ctrl Pts',(17.3277619882547,-20.5361393871241,
15.8034482822256));
#178277=CARTESIAN_POINT('Ctrl Pts',(17.2749437204166,-20.4858982277218,
15.8078248294852));
#178278=CARTESIAN_POINT('Ctrl Pts',(17.2221589491563,-20.4356889305326,
15.8121986012022));
#178279=CARTESIAN_POINT('Ctrl Pts',(17.1719303071397,-20.3827151282831,
15.8165723729191));
#178280=CARTESIAN_POINT('Ctrl Pts',(17.1245538730402,-20.3272716693127,
15.8209461446361));
#178281=CARTESIAN_POINT('Ctrl Pts',(17.0771918557487,-20.2718450819731,
15.8253185853997));
#178282=CARTESIAN_POINT('Ctrl Pts',(17.0326806364326,-20.2139506964276,
15.8296910261632));
#178283=CARTESIAN_POINT('Ctrl Pts',(16.9912774487785,-20.1539180959882,
15.8340634669268));
#178284=CARTESIAN_POINT('Ctrl Pts',(16.9498732024403,-20.0938839605086,
15.8384360194941));
#178285=CARTESIAN_POINT('Ctrl Pts',(16.9115774177713,-20.0317118998147,
15.8428085720614));
#178286=CARTESIAN_POINT('Ctrl Pts',(16.8766042803955,-19.9677608679187,
15.8471811246288));
#178287=CARTESIAN_POINT('Ctrl Pts',(16.8415948465786,-19.9037434652296,
15.8515582151961));
#178288=CARTESIAN_POINT('Ctrl Pts',(16.8099151769008,-19.8379438292392,
15.8559353057634));
#178289=CARTESIAN_POINT('Ctrl Pts',(16.7817332906702,-19.7707451957982,
15.8603123963308));
#178290=CARTESIAN_POINT('Ctrl Pts',(16.7535360132656,-19.7035098626894,
15.8646918773897));
#178291=CARTESIAN_POINT('Ctrl Pts',(16.7288404860623,-19.6348744651307,
15.8690713584486));
#178292=CARTESIAN_POINT('Ctrl Pts',(16.7077654290805,-19.5652393200137,
15.8734508395076));
#178293=CARTESIAN_POINT('Ctrl Pts',(16.6866530167017,-19.4954807470694,
15.8778380831673));
#178294=CARTESIAN_POINT('Ctrl Pts',(16.6691740053291,-19.4247193565783,
15.882225326827));
#178295=CARTESIAN_POINT('Ctrl Pts',(16.6553962633247,-19.3533670463298,
15.8866125704867));
#178296=CARTESIAN_POINT('Ctrl Pts',(16.6460287263818,-19.3048543508531,
15.8895954734216));
#178297=CARTESIAN_POINT('Ctrl Pts',(16.6383710944438,-19.2560686843218,
15.8925783763564));
#178298=CARTESIAN_POINT('Ctrl Pts',(16.6324309574258,-19.207140273759,15.8955612792912));
#178299=CARTESIAN_POINT('Ctrl Pts',(16.6222201199426,-19.1230344615427,
15.9006887598533));
#178300=CARTESIAN_POINT('Ctrl Pts',(16.617056776629,-19.0383036553196,15.9058162404154));
#178301=CARTESIAN_POINT('Ctrl Pts',(16.6170004656572,-18.9534041339617,
15.9109437209775));
#178302=CARTESIAN_POINT('',(16.6170004208928,-18.9533349381466,15.6876313477606));
#178303=CARTESIAN_POINT('Ctrl Pts',(16.7454193926287,-18.2258896998479,
14.9318514575852));
#178304=CARTESIAN_POINT('Ctrl Pts',(16.7539898784969,-18.2024179187845,
14.933289470365));
#178305=CARTESIAN_POINT('Ctrl Pts',(16.7629774004005,-18.1790938469297,
14.9347402968244));
#178306=CARTESIAN_POINT('Ctrl Pts',(16.7777126709423,-18.1427842604912,
14.9370362380879));
#178307=CARTESIAN_POINT('Ctrl Pts',(16.7831788110695,-18.129694155967,14.9378716791207));
#178308=CARTESIAN_POINT('Ctrl Pts',(16.7921001473088,-18.1089193795933,
14.9392103624449));
#178309=CARTESIAN_POINT('Ctrl Pts',(16.7954704382948,-18.101198550981,14.9397107178972));
#178310=CARTESIAN_POINT('Ctrl Pts',(16.8015031078548,-18.0876005617751,
14.9405970648266));
#178311=CARTESIAN_POINT('Ctrl Pts',(16.8041464536433,-18.0817150379637,
14.9409824002202));
#178312=CARTESIAN_POINT('Ctrl Pts',(16.8096767348037,-18.0695507221011,
14.941782396109));
#178313=CARTESIAN_POINT('Ctrl Pts',(16.8125675896862,-18.0632738060156,
14.9421971882002));
#178314=CARTESIAN_POINT('Ctrl Pts',(16.8200827102869,-18.0471642848501,
14.9432669153005));
#178315=CARTESIAN_POINT('Ctrl Pts',(16.8247519940797,-18.0373530143986,
14.9439234032379));
#178316=CARTESIAN_POINT('Ctrl Pts',(16.8446948431519,-17.9962665451481,
14.9466939011902));
#178317=CARTESIAN_POINT('Ctrl Pts',(16.8606622630466,-17.9653359690922,
14.9488319833083));
#178318=CARTESIAN_POINT('Ctrl Pts',(16.904394922929,-17.8855130233668,14.9544918278066));
#178319=CARTESIAN_POINT('Ctrl Pts',(16.9333566758698,-17.8373108233625,
14.958053815934));
#178320=CARTESIAN_POINT('Ctrl Pts',(17.0332350965844,-17.6851475752947,
14.9697636289789));
#178321=CARTESIAN_POINT('Ctrl Pts',(17.111503950185,-17.5863432978684,14.9781230573006));
#178322=CARTESIAN_POINT('Ctrl Pts',(17.2668972608481,-17.4225228703116,
14.993000550841));
#178323=CARTESIAN_POINT('Ctrl Pts',(17.3407869996825,-17.3549236006907,
14.9995201462719));
#178324=CARTESIAN_POINT('Ctrl Pts',(17.4267853808941,-17.2867754164596,
15.0062995425205));
#178325=CARTESIAN_POINT('Ctrl Pts',(17.4344245246477,-17.2808068435704,
15.0068951742375));
#178326=CARTESIAN_POINT('Ctrl Pts',(17.445764031804,-17.2720718978711,15.0077693324552));
#178327=CARTESIAN_POINT('Ctrl Pts',(17.4494327578829,-17.2692649229632,
15.0080506243749));
#178328=CARTESIAN_POINT('Ctrl Pts',(17.4559575636467,-17.2643065100323,
15.0085481504069));
#178329=CARTESIAN_POINT('Ctrl Pts',(17.458809932902,-17.2621502792693,15.0087647193588));
#178330=CARTESIAN_POINT('Ctrl Pts',(17.4649328356691,-17.2575460405312,
15.0092276116425));
#178331=CARTESIAN_POINT('Ctrl Pts',(17.4682049867318,-17.2551002759807,
15.0094737787569));
#178332=CARTESIAN_POINT('Ctrl Pts',(17.4772061297981,-17.2484129081427,
15.0101476971184));
#178333=CARTESIAN_POINT('Ctrl Pts',(17.4829495580454,-17.2441906995523,
15.0105741162415));
#178334=CARTESIAN_POINT('Ctrl Pts',(17.5137221087292,-17.2218071938327,
15.0128403481282));
#178335=CARTESIAN_POINT('Ctrl Pts',(17.5391269881891,-17.204165914299,15.014646426112));
#178336=CARTESIAN_POINT('Ctrl Pts',(17.6171834029864,-17.1524608758435,
15.020031900505));
#178337=CARTESIAN_POINT('Ctrl Pts',(17.6709725467387,-17.1201719094805,
15.0235245474624));
#178338=CARTESIAN_POINT('Ctrl Pts',(17.8443350931063,-17.0263166707742,
15.0343589181434));
#178339=CARTESIAN_POINT('Ctrl Pts',(17.9683762754242,-16.9737227332602,
15.0415276660066));
#178340=CARTESIAN_POINT('Ctrl Pts',(18.1354764545173,-16.9209600364709,
15.0512527095806));
#178341=CARTESIAN_POINT('Ctrl Pts',(18.1747299561353,-16.9098025216839,
15.0535399420459));
#178342=CARTESIAN_POINT('Ctrl Pts',(18.2613894649474,-16.8878561283963,
15.058620684093));
#178343=CARTESIAN_POINT('Ctrl Pts',(18.3088928166469,-16.8775521239902,
15.0614259917412));
#178344=CARTESIAN_POINT('Ctrl Pts',(18.3691073314938,-16.8666460311403,
15.0650250106284));
#178345=CARTESIAN_POINT('Ctrl Pts',(18.3815281410285,-16.8645107393646,
15.0657696551922));
#178346=CARTESIAN_POINT('Ctrl Pts',(18.4012400690407,-16.8613029570123,
15.0669552616516));
#178347=CARTESIAN_POINT('Ctrl Pts',(18.408519118623,-16.8601573933581,15.0673939008005));
#178348=CARTESIAN_POINT('Ctrl Pts',(18.4220931019255,-16.8580937091542,
15.0682134771367));
#178349=CARTESIAN_POINT('Ctrl Pts',(18.4283864969468,-16.8571659127048,
15.0685941026791));
#178350=CARTESIAN_POINT('Ctrl Pts',(18.4423736159789,-16.8551682495619,
15.0694415068844));
#178351=CARTESIAN_POINT('Ctrl Pts',(18.4500692114948,-16.8541123380093,
15.069908721841));
#178352=CARTESIAN_POINT('Ctrl Pts',(18.4724466377461,-16.851167316905,15.0712702319319));
#178353=CARTESIAN_POINT('Ctrl Pts',(18.4871424631253,-16.8493898452894,
15.0721680353832));
#178354=CARTESIAN_POINT('Ctrl Pts',(18.6040634087039,-16.8364908184537,
15.0793414001929));
#178355=CARTESIAN_POINT('Ctrl Pts',(18.7069418159813,-16.8326781665324,
15.0858477816265));
#178356=CARTESIAN_POINT('Ctrl Pts',(18.965368629394,-16.8419222242805,15.1026338888025));
#178357=CARTESIAN_POINT('Ctrl Pts',(19.1199577291818,-16.8646589701208,
15.1131041057439));
#178358=CARTESIAN_POINT('Ctrl Pts',(19.3214646282975,-16.9174646787792,
15.126560009598));
#178359=CARTESIAN_POINT('Ctrl Pts',(19.3717727497202,-16.9326695224225,
15.1298978648114));
#178360=CARTESIAN_POINT('Ctrl Pts',(19.4296851269129,-16.9525534015036,
15.1336748205914));
#178361=CARTESIAN_POINT('Ctrl Pts',(19.4378857908484,-16.955425609842,15.1342080917586));
#178362=CARTESIAN_POINT('Ctrl Pts',(19.4502843211664,-16.9598539687521,
15.1350117163951));
#178363=CARTESIAN_POINT('Ctrl Pts',(19.4544952026125,-16.9613730378522,
15.1352841886319));
#178364=CARTESIAN_POINT('Ctrl Pts',(19.4620494556115,-16.9641253337935,
15.135772129925));
#178365=CARTESIAN_POINT('Ctrl Pts',(19.4653945443353,-16.9653536501286,
15.1359878848015));
#178366=CARTESIAN_POINT('Ctrl Pts',(19.472661416482,-16.968042887147,15.1364559127081));
#178367=CARTESIAN_POINT('Ctrl Pts',(19.4765819616605,-16.9695069874646,
15.1367079928655));
#178368=CARTESIAN_POINT('Ctrl Pts',(19.487595219813,-16.9736570659245,15.1374149860329));
#178369=CARTESIAN_POINT('Ctrl Pts',(19.4946779603429,-16.9763695779007,
15.1378683410873));
#178370=CARTESIAN_POINT('Ctrl Pts',(19.5371983186418,-16.9929163730567,
15.1405829201818));
#178371=CARTESIAN_POINT('Ctrl Pts',(19.5722747537141,-17.0076666850721,
15.1427926120918));
#178372=CARTESIAN_POINT('Ctrl Pts',(19.6869971606401,-17.0595919727712,
15.1499806666271));
#178373=CARTESIAN_POINT('Ctrl Pts',(19.7647300150421,-17.1007815328418,
15.1547896820693));
#178374=CARTESIAN_POINT('Ctrl Pts',(19.9882626432145,-17.23768638006,15.1690493655377));
#178375=CARTESIAN_POINT('Ctrl Pts',(20.1250233222925,-17.346667222233,15.1784223751174));
#178376=CARTESIAN_POINT('Ctrl Pts',(20.2630319169469,-17.4876628575787,
15.1898859632073));
#178377=CARTESIAN_POINT('Ctrl Pts',(20.2789076767094,-17.5044219957036,
15.1912382672544));
#178378=CARTESIAN_POINT('Ctrl Pts',(20.3009669070879,-17.528484937568,15.1931673748106));
#178379=CARTESIAN_POINT('Ctrl Pts',(20.3073801376038,-17.5355765608708,
15.1937344020104));
#178380=CARTESIAN_POINT('Ctrl Pts',(20.3177190137002,-17.5471659450041,
15.1946587518003));
#178381=CARTESIAN_POINT('Ctrl Pts',(20.321674106934,-17.5516373450142,15.1950148328205));
#178382=CARTESIAN_POINT('Ctrl Pts',(20.3299107460889,-17.561028961372,15.195761622865));
#178383=CARTESIAN_POINT('Ctrl Pts',(20.3341885660916,-17.5659523488508,
15.196152481349));
#178384=CARTESIAN_POINT('Ctrl Pts',(20.3443064351711,-17.5777063820968,
15.1970841584231));
#178385=CARTESIAN_POINT('Ctrl Pts',(20.3501258395364,-17.5845545604108,
15.1976258199015));
#178386=CARTESIAN_POINT('Ctrl Pts',(20.3695622157234,-17.6077243391253,
15.1994547284389));
#178387=CARTESIAN_POINT('Ctrl Pts',(20.3829765887197,-17.6242135065956,
15.2007501645598));
#178388=CARTESIAN_POINT('Ctrl Pts',(20.4545184434044,-17.714910408525,15.2078448722442));
#178389=CARTESIAN_POINT('Ctrl Pts',(20.5078810142697,-17.7927259127434,
15.2138291957854));
#178390=CARTESIAN_POINT('Ctrl Pts',(20.6403914491075,-18.0166399543896,
15.2307281692643));
#178391=CARTESIAN_POINT('Ctrl Pts',(20.7078162865442,-18.168882804642,15.2419109716618));
#178392=CARTESIAN_POINT('Ctrl Pts',(20.769161436931,-18.3675594989172,15.2552398700389));
#178393=CARTESIAN_POINT('Ctrl Pts',(20.7803558491844,-18.4080505025665,
15.2578907606393));
#178394=CARTESIAN_POINT('Ctrl Pts',(20.792106572206,-18.4560749532719,15.2609373330676));
#178395=CARTESIAN_POINT('Ctrl Pts',(20.7938361672691,-18.4633086022078,
15.2613936389829));
#178396=CARTESIAN_POINT('Ctrl Pts',(20.7965741903848,-18.4750326150644,
15.2621288594024));
#178397=CARTESIAN_POINT('Ctrl Pts',(20.7976061437692,-18.4795173426932,
15.2624090739161));
#178398=CARTESIAN_POINT('Ctrl Pts',(20.7994135294787,-18.4874908777551,
15.2629054110361));
#178399=CARTESIAN_POINT('Ctrl Pts',(20.8001947580573,-18.4909783141237,
15.263121862514));
#178400=CARTESIAN_POINT('Ctrl Pts',(20.8018524619569,-18.498467228507,15.2635852994625));
#178401=CARTESIAN_POINT('Ctrl Pts',(20.8027261536057,-18.5024692654762,
15.2638321245483));
#178402=CARTESIAN_POINT('Ctrl Pts',(20.8050989856604,-18.5134917056192,
15.2645097029506));
#178403=CARTESIAN_POINT('Ctrl Pts',(20.8065740581177,-18.5205173124898,
15.264939099931));
#178404=CARTESIAN_POINT('Ctrl Pts',(20.8143549360015,-18.5585374801061,
15.2672500908868));
#178405=CARTESIAN_POINT('Ctrl Pts',(20.8200016235565,-18.5896646818428,
15.2690963516887));
#178406=CARTESIAN_POINT('Ctrl Pts',(20.8505127930543,-18.7823525349615,
15.2803089243486));
#178407=CARTESIAN_POINT('Ctrl Pts',(20.8572959209056,-18.9462309529907,
15.2889470804902));
#178408=CARTESIAN_POINT('Ctrl Pts',(20.8364521778122,-19.2260284817361,
15.3043057680651));
#178409=CARTESIAN_POINT('Ctrl Pts',(20.818085161711,-19.3418467941423,15.310841027446));
#178410=CARTESIAN_POINT('Ctrl Pts',(20.7868423563593,-19.4694278260755,
15.3185359648139));
#178411=CARTESIAN_POINT('Ctrl Pts',(20.7833021630712,-19.4832757521026,
15.3193776637806));
#178412=CARTESIAN_POINT('Ctrl Pts',(20.7774449089722,-19.5052570850802,
15.3207244921903));
#178413=CARTESIAN_POINT('Ctrl Pts',(20.7752188322162,-19.5134144405317,
15.3212266787146));
#178414=CARTESIAN_POINT('Ctrl Pts',(20.7712067808673,-19.52777706159,15.3221151562499));
#178415=CARTESIAN_POINT('Ctrl Pts',(20.7694411640473,-19.5339879371094,
15.3225007809202));
#178416=CARTESIAN_POINT('Ctrl Pts',(20.765730681969,-19.546816791544,15.3233002830423));
#178417=CARTESIAN_POINT('Ctrl Pts',(20.7637818324674,-19.5534335294864,
15.3237142866932));
#178418=CARTESIAN_POINT('Ctrl Pts',(20.7586966803705,-19.5703923897565,
15.3247796707361));
#178419=CARTESIAN_POINT('Ctrl Pts',(20.7555134858669,-19.5807201403548,
15.325432579931));
#178420=CARTESIAN_POINT('Ctrl Pts',(20.7419000498259,-19.6237159947741,
15.328168187452));
#178421=CARTESIAN_POINT('Ctrl Pts',(20.7307563656462,-19.6561511115615,
15.3302742074545));
#178422=CARTESIAN_POINT('Ctrl Pts',(20.6996742239813,-19.7399386847355,
15.3358289959565));
#178423=CARTESIAN_POINT('Ctrl Pts',(20.678511633313,-19.7908064221735,15.3393161552602));
#178424=CARTESIAN_POINT('Ctrl Pts',(20.6094731179962,-19.9400546181705,
15.3498858328151));
#178425=CARTESIAN_POINT('Ctrl Pts',(20.5559342362382,-20.0356067170176,
15.3571167414476));
#178426=CARTESIAN_POINT('Ctrl Pts',(20.4696764998539,-20.1649476915121,
15.3673864091129));
#178427=CARTESIAN_POINT('Ctrl Pts',(20.4428466986765,-20.2024631831195,
15.3704265460418));
#178428=CARTESIAN_POINT('Ctrl Pts',(20.4015473052407,-20.2563968172339,
15.3748628270667));
#178429=CARTESIAN_POINT('Ctrl Pts',(20.3880145998484,-20.2735145936583,
15.3762810095849));
#178430=CARTESIAN_POINT('Ctrl Pts',(20.3415255029232,-20.3304864629098,
15.3810282506029));
#178431=CARTESIAN_POINT('Ctrl Pts',(20.3073715064803,-20.3693447809194,
15.3843123436245));
#178432=CARTESIAN_POINT('Ctrl Pts',(20.2658813861545,-20.413199243317,15.3880359756918));
#178433=CARTESIAN_POINT('Ctrl Pts',(20.2598985749258,-20.4194458609474,
15.3885667885746));
#178434=CARTESIAN_POINT('Ctrl Pts',(20.2507673997294,-20.4288634389345,
15.3893674502862));
#178435=CARTESIAN_POINT('Ctrl Pts',(20.2476470881257,-20.4320613012977,
15.3896393950357));
#178436=CARTESIAN_POINT('Ctrl Pts',(20.2420203092301,-20.4377915202144,
15.3901267748702));
#178437=CARTESIAN_POINT('Ctrl Pts',(20.2395175646328,-20.4403274363343,
15.3903424928276));
#178438=CARTESIAN_POINT('Ctrl Pts',(20.23405649581,-20.4458330158099,15.3908108816896));
#178439=CARTESIAN_POINT('Ctrl Pts',(20.2310957600289,-20.4488002056881,
15.3910633573256));
#178440=CARTESIAN_POINT('Ctrl Pts',(20.2227314768663,-20.4571330764128,
15.3917725791028));
#178441=CARTESIAN_POINT('Ctrl Pts',(20.2173077001495,-20.4624784866368,
15.3922277514971));
#178442=CARTESIAN_POINT('Ctrl Pts',(20.1842244755602,-20.4947336564113,
15.3949765615158));
#178443=CARTESIAN_POINT('Ctrl Pts',(20.1558604345399,-20.5209141120957,
15.3972171441048));
#178444=CARTESIAN_POINT('Ctrl Pts',(20.0589544815258,-20.6055716758488,
15.4045580810294));
#178445=CARTESIAN_POINT('Ctrl Pts',(19.9873951814078,-20.6604515687314,
15.4094807701987));
#178446=CARTESIAN_POINT('Ctrl Pts',(19.7703838425376,-20.8058842291388,
15.4236858474793));
#178447=CARTESIAN_POINT('Ctrl Pts',(19.617205868654,-20.8835586278959,15.4329071198529));
#178448=CARTESIAN_POINT('Ctrl Pts',(19.4344668356363,-20.9498932474798,
15.4442004818327));
#178449=CARTESIAN_POINT('Ctrl Pts',(19.4124498592442,-20.9574767366913,
15.4455644109655));
#178450=CARTESIAN_POINT('Ctrl Pts',(19.3811909128918,-20.9676698590786,
15.4475072847831));
#178451=CARTESIAN_POINT('Ctrl Pts',(19.3720489314345,-20.9705823280256,
15.4480762603632));
#178452=CARTESIAN_POINT('Ctrl Pts',(19.3571816552308,-20.9752076841959,
15.4490029216618));
#178453=CARTESIAN_POINT('Ctrl Pts',(19.3514682853889,-20.9769586722245,
15.4493593532819));
#178454=CARTESIAN_POINT('Ctrl Pts',(19.3395085365729,-20.9805686788854,
15.4501061775866));
#178455=CARTESIAN_POINT('Ctrl Pts',(19.3332608417802,-20.9824230876476,
15.450496716635));
#178456=CARTESIAN_POINT('Ctrl Pts',(19.3184050206524,-20.9867579767451,
15.4514263441498));
#178457=CARTESIAN_POINT('Ctrl Pts',(19.3097895677072,-20.98921270906,15.4519662656662));
#178458=CARTESIAN_POINT('Ctrl Pts',(19.2808413694828,-20.9972623885439,
15.4537832264802));
#178459=CARTESIAN_POINT('Ctrl Pts',(19.2604411623725,-21.0026080496847,
15.4550683098663));
#178460=CARTESIAN_POINT('Ctrl Pts',(19.1497844519941,-21.029844440252,15.4620661600873));
#178461=CARTESIAN_POINT('Ctrl Pts',(19.0582528190898,-21.0460798449994,
15.4679583697048));
#178462=CARTESIAN_POINT('Ctrl Pts',(18.8138452422157,-21.0730219504027,
15.4839175569266));
#178463=CARTESIAN_POINT('Ctrl Pts',(18.6603709972031,-21.0732459581053,
15.4941952255566));
#178464=CARTESIAN_POINT('Ctrl Pts',(18.504928816888,-21.0565727218587,15.5043123765119));
#178465=CARTESIAN_POINT('Ctrl Pts',(18.5016396530041,-21.0562121133199,
15.5045263010876));
#178466=CARTESIAN_POINT('Ctrl Pts',(18.4463584969669,-21.0500201466498,
15.508119005645));
#178467=CARTESIAN_POINT('Ctrl Pts',(18.3945945228599,-21.0422705749683,
15.5114427770827));
#178468=CARTESIAN_POINT('Ctrl Pts',(18.334640634137,-21.0310085027146,15.51520555058));
#178469=CARTESIAN_POINT('Ctrl Pts',(18.3261244042237,-21.0293545103693,
15.515737968209));
#178470=CARTESIAN_POINT('Ctrl Pts',(18.3132323169734,-21.026768316934,15.5165405642306));
#178471=CARTESIAN_POINT('Ctrl Pts',(18.308848970586,-21.0258745417867,15.5168128534451));
#178472=CARTESIAN_POINT('Ctrl Pts',(18.3009792698467,-21.0242438911216,
15.517300599761));
#178473=CARTESIAN_POINT('Ctrl Pts',(18.2974919301759,-21.0235121053444,
15.5175163416602));
#178474=CARTESIAN_POINT('Ctrl Pts',(18.2899105488846,-21.0219012277284,
15.5179844940444));
#178475=CARTESIAN_POINT('Ctrl Pts',(18.2858172758937,-21.0210187963508,
15.5182367108281));
#178476=CARTESIAN_POINT('Ctrl Pts',(18.274307120353,-21.0185016665517,15.518944473656));
#178477=CARTESIAN_POINT('Ctrl Pts',(18.2668962910998,-21.0168391730474,
15.5193984562993));
#178478=CARTESIAN_POINT('Ctrl Pts',(18.2222370765169,-21.0065678980349,
15.522124791579));
#178479=CARTESIAN_POINT('Ctrl Pts',(18.1852159989921,-20.9969907259359,
15.5243450917027));
#178480=CARTESIAN_POINT('Ctrl Pts',(18.0632993635277,-20.9619017332701,
15.5315853686935));
#178481=CARTESIAN_POINT('Ctrl Pts',(17.9797430098427,-20.9320614146232,
15.5364331799524));
#178482=CARTESIAN_POINT('Ctrl Pts',(17.7392675851407,-20.8287407235072,
15.550669209331));
#178483=CARTESIAN_POINT('Ctrl Pts',(17.5892360359658,-20.7411777446196,
15.5599856754051));
#178484=CARTESIAN_POINT('Ctrl Pts',(17.4330672552499,-20.6222700422172,
15.5713889394683));
#178485=CARTESIAN_POINT('Ctrl Pts',(17.4148286011103,-20.6079030098277,
15.5727489053254));
#178486=CARTESIAN_POINT('Ctrl Pts',(17.3894007872719,-20.5871861660199,
15.5746870842445));
#178487=CARTESIAN_POINT('Ctrl Pts',(17.3820124270668,-20.5810826984707,
15.5752553941233));
#178488=CARTESIAN_POINT('Ctrl Pts',(17.3700863783538,-20.5710936713861,
15.5761812654653));
#178489=CARTESIAN_POINT('Ctrl Pts',(17.3655231949928,-20.5672386563803,
15.5765375771153));
#178490=CARTESIAN_POINT('Ctrl Pts',(17.3563662784197,-20.5594361616393,
15.5772567650024));
#178491=CARTESIAN_POINT('Ctrl Pts',(17.3517730494286,-20.5554881790995,
15.5776196601031));
#178492=CARTESIAN_POINT('Ctrl Pts',(17.3407758110547,-20.5459534441586,
15.5784937145474));
#178493=CARTESIAN_POINT('Ctrl Pts',(17.3343884149842,-20.5403477675266,
15.5790056581806));
#178494=CARTESIAN_POINT('Ctrl Pts',(17.3141046862124,-20.522329101273,15.5806452238866));
#178495=CARTESIAN_POINT('Ctrl Pts',(17.3003387035503,-20.5097713056291,
15.5817789174205));
#178496=CARTESIAN_POINT('Ctrl Pts',(17.2684734255031,-20.4799225576682,
15.5844535762565));
#178497=CARTESIAN_POINT('Ctrl Pts',(17.2505117783673,-20.462489356358,15.5860005246433));
#178498=CARTESIAN_POINT('Ctrl Pts',(17.1883633529826,-20.3999914731401,
15.5914949787602));
#178499=CARTESIAN_POINT('Ctrl Pts',(17.1458897746575,-20.3532767985085,
15.5955120527167));
#178500=CARTESIAN_POINT('Ctrl Pts',(17.0460471666817,-20.2330859220675,
15.6056165632377));
#178501=CARTESIAN_POINT('Ctrl Pts',(16.9913226606222,-20.1575868650647,
15.6117716441221));
#178502=CARTESIAN_POINT('Ctrl Pts',(16.8765740252499,-19.9750611031889,
15.6260169947454));
#178503=CARTESIAN_POINT('Ctrl Pts',(16.8205080328898,-19.865915016324,15.6340846131507));
#178504=CARTESIAN_POINT('Ctrl Pts',(16.7706163236359,-19.7437719914218,
15.642232947836));
#178505=CARTESIAN_POINT('Ctrl Pts',(16.7671005791807,-19.7349974604127,
15.6428135502771));
#178506=CARTESIAN_POINT('Ctrl Pts',(16.7619716143272,-19.7219441213306,
15.6436699197268));
#178507=CARTESIAN_POINT('Ctrl Pts',(16.7603133509283,-19.7176833001007,
15.6439482954824));
#178508=CARTESIAN_POINT('Ctrl Pts',(16.7573845202505,-19.7100850856542,
15.6444426143378));
#178509=CARTESIAN_POINT('Ctrl Pts',(16.7561085836893,-19.7067498246512,
15.6446588761142));
#178510=CARTESIAN_POINT('Ctrl Pts',(16.7533801739178,-19.69956340522,15.6451232922391));
#178511=CARTESIAN_POINT('Ctrl Pts',(16.7519304948998,-19.6957112463241,
15.6453712789052));
#178512=CARTESIAN_POINT('Ctrl Pts',(16.7479520837355,-19.6850453566173,
15.6460553299809));
#178513=CARTESIAN_POINT('Ctrl Pts',(16.7454471631092,-19.6782227199235,
15.6464899947657));
#178514=CARTESIAN_POINT('Ctrl Pts',(16.7317897365044,-19.6404235417277,
15.6488828422822));
#178515=CARTESIAN_POINT('Ctrl Pts',(16.7213252060677,-19.609201153953,15.6508026668322));
#178516=CARTESIAN_POINT('Ctrl Pts',(16.6636029018366,-19.4226428511168,
15.6620104021434));
#178517=CARTESIAN_POINT('Ctrl Pts',(16.6336098822308,-19.2625187434697,
15.6705925842714));
#178518=CARTESIAN_POINT('Ctrl Pts',(16.618771005776,-19.0515351732291,15.6821718102302));
#178519=CARTESIAN_POINT('Ctrl Pts',(16.617031386799,-19.0024419403517,15.6848816867355));
#178520=CARTESIAN_POINT('Ctrl Pts',(16.6170004208928,-18.9533349381466,
15.6876313477606));
#178521=CARTESIAN_POINT('Ctrl Pts',(16.6170004192074,-18.9533322627481,
15.6876314975649));
#178522=CARTESIAN_POINT('Ctrl Pts',(16.6169565169202,-18.8835704055676,
15.6915376931939));
#178523=CARTESIAN_POINT('Ctrl Pts',(16.62036089015,-18.8138535640072,15.6955212326732));
#178524=CARTESIAN_POINT('Ctrl Pts',(16.6282125589666,-18.734158587401,15.7002202348787));
#178525=CARTESIAN_POINT('Ctrl Pts',(16.6293001576506,-18.7238899479628,
15.7008284385311));
#178526=CARTESIAN_POINT('Ctrl Pts',(16.6312632475932,-18.7065663360107,
15.7018593087927));
#178527=CARTESIAN_POINT('Ctrl Pts',(16.6320992366459,-18.6995070050852,
15.7022807358949));
#178528=CARTESIAN_POINT('Ctrl Pts',(16.6337047671108,-18.6865103049005,
15.7030591555859));
#178529=CARTESIAN_POINT('Ctrl Pts',(16.6344639731179,-18.6805717144542,
15.7034158195831));
#178530=CARTESIAN_POINT('Ctrl Pts',(16.6360832810977,-18.6683187506339,
15.7041537754714));
#178531=CARTESIAN_POINT('Ctrl Pts',(16.6369467236812,-18.6620048869433,
15.7045351694354));
#178532=CARTESIAN_POINT('Ctrl Pts',(16.6389488845612,-18.6478409232857,
15.7053933353336));
#178533=CARTESIAN_POINT('Ctrl Pts',(16.6401032377709,-18.639993162409,15.7058705976374));
#178534=CARTESIAN_POINT('Ctrl Pts',(16.6431522412091,-18.6200441629729,
15.7070884153629));
#178535=CARTESIAN_POINT('Ctrl Pts',(16.6451078418647,-18.6079526631919,
15.7078308924383));
#178536=CARTESIAN_POINT('Ctrl Pts',(16.6571524976023,-18.5373722396685,
15.7121907850031));
#178537=CARTESIAN_POINT('Ctrl Pts',(16.6695919036022,-18.4793163395534,
15.7158823634575));
#178538=CARTESIAN_POINT('Ctrl Pts',(16.6997698414317,-18.3626461002099,
15.7235211131819));
#178539=CARTESIAN_POINT('Ctrl Pts',(16.7176452909224,-18.3041241696756,
15.7274691240795));
#178540=CARTESIAN_POINT('Ctrl Pts',(16.7404566265233,-18.2395907584607,
15.7319399041205));
#178541=CARTESIAN_POINT('Ctrl Pts',(16.7429205066429,-18.232733338599,15.7324164674271));
#178542=CARTESIAN_POINT('Ctrl Pts',(16.7454193749215,-18.2258897483422,
15.7328935260819));
#178543=CARTESIAN_POINT('Origin',(18.734,-18.952,0.));
#178544=CARTESIAN_POINT('',(16.7454192974512,-18.2258899605083,16.7554728927777));
#178545=CARTESIAN_POINT('',(16.7454193692319,-18.2258897639242,16.5356516076535));
#178546=CARTESIAN_POINT('',(16.7454193692319,-18.2258897639242,0.));
#178547=CARTESIAN_POINT('Ctrl Pts',(16.7454192974512,-18.2258899605083,
16.7554728927777));
#178548=CARTESIAN_POINT('Ctrl Pts',(16.7246695920637,-18.2827166967783,
16.7521869458714));
#178549=CARTESIAN_POINT('Ctrl Pts',(16.7063536199304,-18.3404386255704,
16.7488940241178));
#178550=CARTESIAN_POINT('Ctrl Pts',(16.6648838452894,-18.493651950924,16.7401350888319));
#178551=CARTESIAN_POINT('Ctrl Pts',(16.645861750119,-18.5900612109107,16.7345998833666));
#178552=CARTESIAN_POINT('Ctrl Pts',(16.6317631855524,-18.70199076929,16.7279812705224));
#178553=CARTESIAN_POINT('Ctrl Pts',(16.6300811167997,-18.7165651764132,
16.7271159336786));
#178554=CARTESIAN_POINT('Ctrl Pts',(16.6277432519347,-18.7388535224522,
16.7257867711579));
#178555=CARTESIAN_POINT('Ctrl Pts',(16.6269780369073,-18.7465557149213,
16.7253263933704));
#178556=CARTESIAN_POINT('Ctrl Pts',(16.6257184973669,-18.7599814909001,
16.7245219962028));
#178557=CARTESIAN_POINT('Ctrl Pts',(16.625205197225,-18.7657032448873,16.7241785780139));
#178558=CARTESIAN_POINT('Ctrl Pts',(16.6241033853643,-18.7785735781056,
16.7234047182599));
#178559=CARTESIAN_POINT('Ctrl Pts',(16.6235279049427,-18.7857231757729,
16.7229738710155));
#178560=CARTESIAN_POINT('Ctrl Pts',(16.6220830309384,-18.8048914690991,
16.7218161189399));
#178561=CARTESIAN_POINT('Ctrl Pts',(16.6212799114272,-18.8169147602251,
16.7210871425985));
#178562=CARTESIAN_POINT('Ctrl Pts',(16.6181723376229,-18.8702856926723,
16.7178385079915));
#178563=CARTESIAN_POINT('Ctrl Pts',(16.6169788916296,-18.9116865673218,
16.7152843363529));
#178564=CARTESIAN_POINT('Ctrl Pts',(16.6170878342108,-19.1225723393612,
16.7020917135601));
#178565=CARTESIAN_POINT('Ctrl Pts',(16.6375272228444,-19.2914052006955,
16.6908605394253));
#178566=CARTESIAN_POINT('Ctrl Pts',(16.7025602568232,-19.5567378422221,
16.6728475754346));
#178567=CARTESIAN_POINT('Ctrl Pts',(16.7346397976448,-19.6555760008162,
16.6660710230332));
#178568=CARTESIAN_POINT('Ctrl Pts',(16.7775028814751,-19.7606419935097,
16.6590602329866));
#178569=CARTESIAN_POINT('Ctrl Pts',(16.7812238449539,-19.7695867812862,
16.6584650042628));
#178570=CARTESIAN_POINT('Ctrl Pts',(16.7868091127715,-19.7827574707192,
16.6575913224019));
#178571=CARTESIAN_POINT('Ctrl Pts',(16.7886259927884,-19.7870031733232,
16.6573101081016));
#178572=CARTESIAN_POINT('Ctrl Pts',(16.7918742110331,-19.7945254916574,
16.6568126678403));
#178573=CARTESIAN_POINT('Ctrl Pts',(16.7932999703058,-19.7978044571216,
16.6565961074699));
#178574=CARTESIAN_POINT('Ctrl Pts',(16.7963728344805,-19.8048227613399,
16.6561331765346));
#178575=CARTESIAN_POINT('Ctrl Pts',(16.7980224549729,-19.808560938065,16.6558869624849));
#178576=CARTESIAN_POINT('Ctrl Pts',(16.8025810936737,-19.8188107470481,
16.6552127833076));
#178577=CARTESIAN_POINT('Ctrl Pts',(16.8055122409406,-19.825312561095,16.6547861520224));
#178578=CARTESIAN_POINT('Ctrl Pts',(16.8213484140837,-19.8599715103299,
16.65251676682));
#178579=CARTESIAN_POINT('Ctrl Pts',(16.8348380827748,-19.8878592805146,
16.6507078589996));
#178580=CARTESIAN_POINT('Ctrl Pts',(16.9233519936901,-20.0610449154679,
16.6395212075378));
#178581=CARTESIAN_POINT('Ctrl Pts',(17.0143947885187,-20.1975509179192,
16.6308786888292));
#178582=CARTESIAN_POINT('Ctrl Pts',(17.196466169748,-20.4119804038316,16.6154835501062));
#178583=CARTESIAN_POINT('Ctrl Pts',(17.2800216251338,-20.4952091871193,
16.608913302389));
#178584=CARTESIAN_POINT('Ctrl Pts',(17.380992329486,-20.5802701785601,16.6011789840365));
#178585=CARTESIAN_POINT('Ctrl Pts',(17.3920227713541,-20.5893730893443,
16.6003368065505));
#178586=CARTESIAN_POINT('Ctrl Pts',(17.409722114742,-20.6036805445389,16.598989355451));
#178587=CARTESIAN_POINT('Ctrl Pts',(17.4163315616311,-20.6089581835253,
16.5984870290645));
#178588=CARTESIAN_POINT('Ctrl Pts',(17.4280424983855,-20.6181949771008,
16.5975983885361));
#178589=CARTESIAN_POINT('Ctrl Pts',(17.4331308375226,-20.6221706854176,
16.5972127415187));
#178590=CARTESIAN_POINT('Ctrl Pts',(17.4436912521112,-20.6303443929479,
16.5964132759632));
#178591=CARTESIAN_POINT('Ctrl Pts',(17.4491658059688,-20.6345390510522,
16.5959993316345));
#178592=CARTESIAN_POINT('Ctrl Pts',(17.4632677541215,-20.6452351458732,
16.5949342747658));
#178593=CARTESIAN_POINT('Ctrl Pts',(17.4719245142755,-20.6516973735035,
16.5942816352357));
#178594=CARTESIAN_POINT('Ctrl Pts',(17.5082358322577,-20.6783732399568,
16.591548639891));
#178595=CARTESIAN_POINT('Ctrl Pts',(17.5363282210755,-20.6979795111006,
16.5894450180728));
#178596=CARTESIAN_POINT('Ctrl Pts',(17.6107288172203,-20.747264617646,16.5838980606411));
#178597=CARTESIAN_POINT('Ctrl Pts',(17.65773750538,-20.7758342643689,16.5804164690477));
#178598=CARTESIAN_POINT('Ctrl Pts',(17.8013465148784,-20.8556263858028,
16.5698574889258));
#178599=CARTESIAN_POINT('Ctrl Pts',(17.9008524232842,-20.9012299985079,
16.5626316748121));
#178600=CARTESIAN_POINT('Ctrl Pts',(18.0393939197642,-20.9521700144381,
16.5528807854854));
#178601=CARTESIAN_POINT('Ctrl Pts',(18.0757162153561,-20.9644165205872,
16.550353032336));
#178602=CARTESIAN_POINT('Ctrl Pts',(18.1433460128919,-20.985191624372,16.5457179372652));
#178603=CARTESIAN_POINT('Ctrl Pts',(18.1745562879807,-20.9939998016045,
16.5436063985128));
#178604=CARTESIAN_POINT('Ctrl Pts',(18.2120838153806,-21.0036657907865,
16.5411087272298));
#178605=CARTESIAN_POINT('Ctrl Pts',(18.2182171631365,-21.0052162787845,
16.5407018266001));
#178606=CARTESIAN_POINT('Ctrl Pts',(18.2665317275001,-21.0171998718105,
16.5375072608297));
#178607=CARTESIAN_POINT('Ctrl Pts',(18.3090215578563,-21.0263603873719,
16.5347619590204));
#178608=CARTESIAN_POINT('Ctrl Pts',(18.3591553016936,-21.0355635070149,
16.5316205812639));
#178609=CARTESIAN_POINT('Ctrl Pts',(18.3665514941911,-21.0368805805222,
16.5311596175139));
#178610=CARTESIAN_POINT('Ctrl Pts',(18.3785117016488,-21.0389447656501,
16.5304183816415));
#178611=CARTESIAN_POINT('Ctrl Pts',(18.3830713522644,-21.0397163289763,
16.5301367754393));
#178612=CARTESIAN_POINT('Ctrl Pts',(18.3911615310593,-21.0410580588519,
16.5296389017171));
#178613=CARTESIAN_POINT('Ctrl Pts',(18.3946910093723,-21.0416342260313,
16.5294222976174));
#178614=CARTESIAN_POINT('Ctrl Pts',(18.4022522865027,-21.0428488986275,
16.5289595602004));
#178615=CARTESIAN_POINT('Ctrl Pts',(18.406284465869,-21.0434846859682,16.5287135818993));
#178616=CARTESIAN_POINT('Ctrl Pts',(18.4173486414224,-21.0451964845796,
16.5280407131526));
#178617=CARTESIAN_POINT('Ctrl Pts',(18.4243843361549,-21.0462487316264,
16.5276151479222));
#178618=CARTESIAN_POINT('Ctrl Pts',(18.461834575018,-21.0516568740241,16.5253615574399));
#178619=CARTESIAN_POINT('Ctrl Pts',(18.4923376455223,-21.0553859694736,
16.523566822637));
#178620=CARTESIAN_POINT('Ctrl Pts',(18.5846792262413,-21.0646395112173,
16.5182275421597));
#178621=CARTESIAN_POINT('Ctrl Pts',(18.6466926646594,-21.0681098622425,
16.5147680059268));
#178622=CARTESIAN_POINT('Ctrl Pts',(18.8556388020453,-21.0705999193564,
16.5032794219685));
#178623=CARTESIAN_POINT('Ctrl Pts',(19.0022847612066,-21.0570619012732,
16.4954668615935));
#178624=CARTESIAN_POINT('Ctrl Pts',(19.2195938395234,-21.0139078096739,
16.4830959578587));
#178625=CARTESIAN_POINT('Ctrl Pts',(19.2920097291687,-20.9954991035761,
16.4788410329755));
#178626=CARTESIAN_POINT('Ctrl Pts',(19.3758190961901,-20.9694065653792,
16.4736906390922));
#178627=CARTESIAN_POINT('Ctrl Pts',(19.3883045083419,-20.9653918150907,
16.4729174212191));
#178628=CARTESIAN_POINT('Ctrl Pts',(19.4085312642726,-20.9586797854283,
16.4716547581577));
#178629=CARTESIAN_POINT('Ctrl Pts',(19.4162957788978,-20.9560530569173,
16.4711676383336));
#178630=CARTESIAN_POINT('Ctrl Pts',(19.4300950343634,-20.951295290973,16.4702975271425));
#178631=CARTESIAN_POINT('Ctrl Pts',(19.4361357656776,-20.9491818451356,
16.4699151228316));
#178632=CARTESIAN_POINT('Ctrl Pts',(19.44884398157,-20.9446708922582,16.4691074187185));
#178633=CARTESIAN_POINT('Ctrl Pts',(19.4555091875467,-20.9422672416602,
16.4686819181977));
#178634=CARTESIAN_POINT('Ctrl Pts',(19.4731068882467,-20.9358210273962,
16.467553465513));
#178635=CARTESIAN_POINT('Ctrl Pts',(19.4840181638137,-20.9317215982123,
16.466848620884));
#178636=CARTESIAN_POINT('Ctrl Pts',(19.5345545425301,-20.9122570365838,
16.4635596353019));
#178637=CARTESIAN_POINT('Ctrl Pts',(19.5737427897822,-20.8957918774756,
16.4609387457589));
#178638=CARTESIAN_POINT('Ctrl Pts',(19.6803243755859,-20.8471863477512,
16.4536089749656));
#178639=CARTESIAN_POINT('Ctrl Pts',(19.7465497052036,-20.812645673675,16.4488238339975));
#178640=CARTESIAN_POINT('Ctrl Pts',(19.8888734742627,-20.7285634160326,
16.4380545960301));
#178641=CARTESIAN_POINT('Ctrl Pts',(19.9638932674497,-20.6774772302302,
16.4320430114774));
#178642=CARTESIAN_POINT('Ctrl Pts',(20.1201754941372,-20.5556702515601,
16.4189701264334));
#178643=CARTESIAN_POINT('Ctrl Pts',(20.1998034725076,-20.4832303688943,
16.4119383050303));
#178644=CARTESIAN_POINT('Ctrl Pts',(20.2802157596568,-20.3980286880123,
16.4047004456004));
#178645=CARTESIAN_POINT('Ctrl Pts',(20.2867920040622,-20.3909646076896,
16.4041074892436));
#178646=CARTESIAN_POINT('Ctrl Pts',(20.2964385206063,-20.3804593554748,
16.4032364942098));
#178647=CARTESIAN_POINT('Ctrl Pts',(20.2995461201574,-20.3770528437594,
16.4029557183089));
#178648=CARTESIAN_POINT('Ctrl Pts',(20.3050431785446,-20.3709873537681,
16.4024587622354));
#178649=CARTESIAN_POINT('Ctrl Pts',(20.3074370541459,-20.3683324526115,
16.4022422500809));
#178650=CARTESIAN_POINT('Ctrl Pts',(20.3125557152281,-20.3626266641098,
16.4017790994339));
#178651=CARTESIAN_POINT('Ctrl Pts',(20.3152783791295,-20.3595739482974,
16.4015326191452));
#178652=CARTESIAN_POINT('Ctrl Pts',(20.3227373011253,-20.3511618712906,
16.4008569593889));
#178653=CARTESIAN_POINT('Ctrl Pts',(20.3274553248212,-20.3457863125969,
16.4004291235405));
#178654=CARTESIAN_POINT('Ctrl Pts',(20.3526454098058,-20.3167904779122,
16.3981417303946));
#178655=CARTESIAN_POINT('Ctrl Pts',(20.3726208588295,-20.2927415583613,
16.3963166586658));
#178656=CARTESIAN_POINT('Ctrl Pts',(20.4938881886454,-20.1399840740441,
16.3851021957151));
#178657=CARTESIAN_POINT('Ctrl Pts',(20.5805004428922,-20.0003134258405,
16.3764475570268));
#178658=CARTESIAN_POINT('Ctrl Pts',(20.6999637618455,-19.7459808249813,
16.3610664055762));
#178659=CARTESIAN_POINT('Ctrl Pts',(20.7408830393391,-19.6359840904026,
16.3545261415905));
#178660=CARTESIAN_POINT('Ctrl Pts',(20.7763480645627,-19.509411619263,16.3468255708633));
#178661=CARTESIAN_POINT('Ctrl Pts',(20.7800651782993,-19.4956088679742,
16.3459838010905));
#178662=CARTESIAN_POINT('Ctrl Pts',(20.7857582392627,-19.4735828139439,
16.3446368805025));
#178663=CARTESIAN_POINT('Ctrl Pts',(20.7878252239812,-19.4653833366579,
16.344134673243));
#178664=CARTESIAN_POINT('Ctrl Pts',(20.7913838268615,-19.4509012751989,
16.3432461714996));
#178665=CARTESIAN_POINT('Ctrl Pts',(20.7928959373918,-19.4446238027058,
16.3428605434722));
#178666=CARTESIAN_POINT('Ctrl Pts',(20.795963893721,-19.4316263948014,16.3420610466401));
#178667=CARTESIAN_POINT('Ctrl Pts',(20.7975156612635,-19.4249055842003,
16.3416470516966));
#178668=CARTESIAN_POINT('Ctrl Pts',(20.8014142116704,-19.4076361032048,
16.3405817158572));
#178669=CARTESIAN_POINT('Ctrl Pts',(20.803713097208,-19.397076925514,16.3399288464261));
#178670=CARTESIAN_POINT('Ctrl Pts',(20.8129681953377,-19.3529436891469,
16.3371936247649));
#178671=CARTESIAN_POINT('Ctrl Pts',(20.81918876568,-19.3192222686824,16.33508795909));
#178672=CARTESIAN_POINT('Ctrl Pts',(20.8332586100318,-19.23098823302,16.3295343279965));
#178673=CARTESIAN_POINT('Ctrl Pts',(20.8398041894306,-19.1762967732665,
16.3260479917225));
#178674=CARTESIAN_POINT('Ctrl Pts',(20.8529620952653,-19.0124045270463,
16.315479895195));
#178675=CARTESIAN_POINT('Ctrl Pts',(20.8532530398053,-18.9028863096366,
16.3082497393259));
#178676=CARTESIAN_POINT('Ctrl Pts',(20.8362310514469,-18.6756725496535,
16.2931984531219));
#178677=CARTESIAN_POINT('Ctrl Pts',(20.8174699425562,-18.5584370576244,
16.285405373538));
#178678=CARTESIAN_POINT('Ctrl Pts',(20.7867038640797,-18.4341326998506,
16.2774959409879));
#178679=CARTESIAN_POINT('Ctrl Pts',(20.7843534156278,-18.4249036397557,
16.2769109240264));
#178680=CARTESIAN_POINT('Ctrl Pts',(20.7807789197147,-18.4112541397232,
16.2760493247114));
#178681=CARTESIAN_POINT('Ctrl Pts',(20.7796026961359,-18.4068214585382,
16.2757700880254));
#178682=CARTESIAN_POINT('Ctrl Pts',(20.7774846398149,-18.398942780428,16.2752748258948));
#178683=CARTESIAN_POINT('Ctrl Pts',(20.7765484816545,-18.3954953171535,
16.2750584769984));
#178684=CARTESIAN_POINT('Ctrl Pts',(20.7745173849428,-18.3880898425376,
16.2745945271954));
#178685=CARTESIAN_POINT('Ctrl Pts',(20.7734196581763,-18.3841326541823,
16.2743470905249));
#178686=CARTESIAN_POINT('Ctrl Pts',(20.7703587304061,-18.3732216923779,
16.2736661061644));
#178687=CARTESIAN_POINT('Ctrl Pts',(20.7683714114672,-18.3662746617194,
16.2732339375138));
#178688=CARTESIAN_POINT('Ctrl Pts',(20.7573053281698,-18.3283270092134,
16.2708803157118));
#178689=CARTESIAN_POINT('Ctrl Pts',(20.7475529738977,-18.29752530341,16.268995754699));
#178690=CARTESIAN_POINT('Ctrl Pts',(20.6843927193559,-18.1128416537301,
16.2577860268716));
#178691=CARTESIAN_POINT('Ctrl Pts',(20.6140714909384,-17.9653077440627,
16.2491772491913));
#178692=CARTESIAN_POINT('Ctrl Pts',(20.4654113158115,-17.7282476763719,
16.2338590457182));
#178693=CARTESIAN_POINT('Ctrl Pts',(20.3952164074734,-17.6345366516259,
16.2273331984634));
#178694=CARTESIAN_POINT('Ctrl Pts',(20.3081688892259,-17.5364133593976,
16.219648855837));
#178695=CARTESIAN_POINT('Ctrl Pts',(20.2985772719514,-17.5258193753807,
16.2188072917872));
#178696=CARTESIAN_POINT('Ctrl Pts',(20.283141426536,-17.5091135431319,16.2174606388905));
#178697=CARTESIAN_POINT('Ctrl Pts',(20.2773664646587,-17.5029380829562,
16.2169584917476));
#178698=CARTESIAN_POINT('Ctrl Pts',(20.2671163414441,-17.4921078893121,
16.2160700600332));
#178699=CARTESIAN_POINT('Ctrl Pts',(20.262656562493,-17.4874386992094,16.2156844415814));
#178700=CARTESIAN_POINT('Ctrl Pts',(20.2533882317986,-17.4778236250631,
16.2148849289276));
#178701=CARTESIAN_POINT('Ctrl Pts',(20.2485767326516,-17.4728807003799,
16.2144709084111));
#178702=CARTESIAN_POINT('Ctrl Pts',(20.2361643841556,-17.4602533776872,
16.2134054316305));
#178703=CARTESIAN_POINT('Ctrl Pts',(20.2285287562794,-17.4526035840792,
16.2127524460503));
#178704=CARTESIAN_POINT('Ctrl Pts',(20.1964160069067,-17.4209202648625,
16.2100160989504));
#178705=CARTESIAN_POINT('Ctrl Pts',(20.1714162540278,-17.3974260940714,
16.2079093999838));
#178706=CARTESIAN_POINT('Ctrl Pts',(20.1047998787551,-17.3378027188554,
16.2023523939175));
#178707=CARTESIAN_POINT('Ctrl Pts',(20.0623259134757,-17.3026744963841,
16.1988636577931));
#178708=CARTESIAN_POINT('Ctrl Pts',(19.931579391767,-17.2028689848442,16.1882909511582));
#178709=CARTESIAN_POINT('Ctrl Pts',(19.8396177042695,-17.1433370314395,
16.1810586003525));
#178710=CARTESIAN_POINT('Ctrl Pts',(19.6394021637277,-17.0347219378359,
16.1660121017659));
#178711=CARTESIAN_POINT('Ctrl Pts',(19.5307614638837,-16.9870862760845,
16.1582260025326));
#178712=CARTESIAN_POINT('Ctrl Pts',(19.4096763404152,-16.9456995868945,
16.1503221520732));
#178713=CARTESIAN_POINT('Ctrl Pts',(19.400635464455,-16.9426774699008,16.1497365788605));
#178714=CARTESIAN_POINT('Ctrl Pts',(19.3872134494329,-16.9382914219884,
16.1488743208427));
#178715=CARTESIAN_POINT('Ctrl Pts',(19.3828479385061,-16.9368805491264,
16.1485949759355));
#178716=CARTESIAN_POINT('Ctrl Pts',(19.3750749336323,-16.934396299578,16.1480995950186));
#178717=CARTESIAN_POINT('Ctrl Pts',(19.3716692813514,-16.9333173476821,
16.147883234957));
#178718=CARTESIAN_POINT('Ctrl Pts',(19.3643440047434,-16.9310169990452,
16.1474193427833));
#178719=CARTESIAN_POINT('Ctrl Pts',(19.3604235654339,-16.9297983849795,
16.1471719744778));
#178720=CARTESIAN_POINT('Ctrl Pts',(19.3495984891982,-16.9264680618227,
16.1464913710623));
#178721=CARTESIAN_POINT('Ctrl Pts',(19.3426864810158,-16.9243802368974,
16.1460595124438));
#178722=CARTESIAN_POINT('Ctrl Pts',(19.3048667972504,-16.9131673341792,
16.143710706958));
#178723=CARTESIAN_POINT('Ctrl Pts',(19.2737627214024,-16.9047130149783,
16.1418304743107));
#178724=CARTESIAN_POINT('Ctrl Pts',(19.084302385453,-16.8578348231362,16.130620460864));
#178725=CARTESIAN_POINT('Ctrl Pts',(18.9221229484456,-16.8370859915432,
16.1220083890275));
#178726=CARTESIAN_POINT('Ctrl Pts',(18.6422407540804,-16.8337601729077,
16.1066856179914));
#178727=CARTESIAN_POINT('Ctrl Pts',(18.5254286060972,-16.842058667023,16.1001586842392));
#178728=CARTESIAN_POINT('Ctrl Pts',(18.3957845843667,-16.8621426916598,
16.0924731185701));
#178729=CARTESIAN_POINT('Ctrl Pts',(18.3816846916261,-16.8644734384523,
16.0916315388002));
#178730=CARTESIAN_POINT('Ctrl Pts',(18.3592822550857,-16.8684100451873,
16.0902848654482));
#178731=CARTESIAN_POINT('Ctrl Pts',(18.3509637154792,-16.8699232267453,
16.0897827137114));
#178732=CARTESIAN_POINT('Ctrl Pts',(18.3363089489912,-16.8726797939313,
16.0888942766458));
#178733=CARTESIAN_POINT('Ctrl Pts',(18.3299688924155,-16.8739024194961,
16.0885086574623));
#178734=CARTESIAN_POINT('Ctrl Pts',(18.3168673832569,-16.8764911556537,
16.0877091460186));
#178735=CARTESIAN_POINT('Ctrl Pts',(18.3101068235671,-16.8778613459722,
16.0872951274571));
#178736=CARTESIAN_POINT('Ctrl Pts',(18.2927708472212,-16.881463196703,16.0862296614504));
#178737=CARTESIAN_POINT('Ctrl Pts',(18.2822057020248,-16.8837428291913,
16.0855766847489));
#178738=CARTESIAN_POINT('Ctrl Pts',(18.2381843929082,-16.8935946634145,
16.0828404236966));
#178739=CARTESIAN_POINT('Ctrl Pts',(18.2048988366685,-16.9018982004212,
16.0807338037345));
#178740=CARTESIAN_POINT('Ctrl Pts',(18.1187106915936,-16.9256377596298,
16.0751770557398));
#178741=CARTESIAN_POINT('Ctrl Pts',(18.0661856584287,-16.9423363349094,
16.0716885031325));
#178742=CARTESIAN_POINT('Ctrl Pts',(17.8184620016038,-17.031876164015,16.0547573725747));
#178743=CARTESIAN_POINT('Ctrl Pts',(17.6341000533558,-17.1312055117576,
16.0405669002422));
#178744=CARTESIAN_POINT('Ctrl Pts',(17.4635919109797,-17.2585500366682,
16.027150434105));
#178745=CARTESIAN_POINT('Ctrl Pts',(17.4599737511049,-17.2612703915826,
16.0268656545933));
#178746=CARTESIAN_POINT('Ctrl Pts',(17.4399959236207,-17.2763914940188,
16.0252928906516));
#178747=CARTESIAN_POINT('Ctrl Pts',(17.4238078904053,-17.2890186040663,
16.0240172019346));
#178748=CARTESIAN_POINT('Ctrl Pts',(17.4027810234203,-17.3059178066909,
16.0223613078333));
#178749=CARTESIAN_POINT('Ctrl Pts',(17.3977750186683,-17.3099788818406,
16.0219671635049));
#178750=CARTESIAN_POINT('Ctrl Pts',(17.3897442068621,-17.316554851155,16.0213351100327));
#178751=CARTESIAN_POINT('Ctrl Pts',(17.3867077693656,-17.3190553842454,
16.0210961889251));
#178752=CARTESIAN_POINT('Ctrl Pts',(17.3810359129483,-17.3237527981171,
16.0206500373336));
#178753=CARTESIAN_POINT('Ctrl Pts',(17.3783988647879,-17.3259476227316,
16.0204426643857));
#178754=CARTESIAN_POINT('Ctrl Pts',(17.3721624817998,-17.3311639015387,
16.0199523607955));
#178755=CARTESIAN_POINT('Ctrl Pts',(17.3685678277111,-17.3341909667995,
16.0196698390166));
#178756=CARTESIAN_POINT('Ctrl Pts',(17.3573349023048,-17.3437143436269,
16.0187871603079));
#178757=CARTESIAN_POINT('Ctrl Pts',(17.3497325578077,-17.3502530783282,
16.0181900230108));
#178758=CARTESIAN_POINT('Ctrl Pts',(17.3319067038273,-17.365806707011,16.016789671789));
#178759=CARTESIAN_POINT('Ctrl Pts',(17.3217231164897,-17.3748669053311,
16.015989523897));
#178760=CARTESIAN_POINT('Ctrl Pts',(17.2863072542557,-17.4069940449287,
16.0132033315157));
#178761=CARTESIAN_POINT('Ctrl Pts',(17.2615457343291,-17.4305742299714,
16.0112489914483));
#178762=CARTESIAN_POINT('Ctrl Pts',(17.183673151494,-17.5084145709385,16.0050398775088));
#178763=CARTESIAN_POINT('Ctrl Pts',(17.1329038446143,-17.5649366684851,
16.0008918747454));
#178764=CARTESIAN_POINT('Ctrl Pts',(16.977365602455,-17.7580482698994,15.9874070852766));
#178765=CARTESIAN_POINT('Ctrl Pts',(16.8861986078455,-17.9046660899658,
15.9781418734426));
#178766=CARTESIAN_POINT('Ctrl Pts',(16.8039952049217,-18.0817643010186,
15.9667990944902));
#178767=CARTESIAN_POINT('Ctrl Pts',(16.7945621974466,-18.1029949187229,
15.9654383085152));
#178768=CARTESIAN_POINT('Ctrl Pts',(16.7817332916145,-18.1331986902603,
15.9634991581719));
#178769=CARTESIAN_POINT('Ctrl Pts',(16.7780458573277,-18.1420467466132,
15.9629307106105));
#178770=CARTESIAN_POINT('Ctrl Pts',(16.7721580878062,-18.1564492469223,
15.9620046758582));
#178771=CARTESIAN_POINT('Ctrl Pts',(16.7699209242609,-18.1619885619307,
15.9616483393663));
#178772=CARTESIAN_POINT('Ctrl Pts',(16.7652917993662,-18.1735916806907,
15.9609015251491));
#178773=CARTESIAN_POINT('Ctrl Pts',(16.7629043418377,-18.1796572032372,
15.9605109002237));
#178774=CARTESIAN_POINT('Ctrl Pts',(16.7572996251138,-18.1940916825968,
15.959580720751));
#178775=CARTESIAN_POINT('Ctrl Pts',(16.7541074642866,-18.2024701921705,
15.9590403305058));
#178776=CARTESIAN_POINT('Ctrl Pts',(16.74909993319,-18.2158687493782,15.9581753499659));
#178777=CARTESIAN_POINT('Ctrl Pts',(16.7472501565826,-18.2208758306612,
15.9578519244208));
#178778=CARTESIAN_POINT('Ctrl Pts',(16.7454193691904,-18.2258897640378,
15.9575278689401));
#178779=CARTESIAN_POINT('Ctrl Pts',(16.7454193749215,-18.2258897483422,
15.7328935260819));
#178780=CARTESIAN_POINT('Ctrl Pts',(16.7986491770761,-18.0801105736236,
15.7430556214707));
#178781=CARTESIAN_POINT('Ctrl Pts',(16.8677533973363,-17.9406091845295,
15.7534873781281));
#178782=CARTESIAN_POINT('Ctrl Pts',(16.969167748649,-17.782329829287,15.7654348139467));
#178783=CARTESIAN_POINT('Ctrl Pts',(16.9874713599678,-17.7551712038437,
15.7674874144511));
#178784=CARTESIAN_POINT('Ctrl Pts',(17.0105923652516,-17.7225254090454,
15.7699474626286));
#178785=CARTESIAN_POINT('Ctrl Pts',(17.0148163996346,-17.7166258068677,
15.7703917328071));
#178786=CARTESIAN_POINT('Ctrl Pts',(17.0214824326368,-17.7074159329509,
15.7710846623438));
#178787=CARTESIAN_POINT('Ctrl Pts',(17.0239038427826,-17.7040909279055,
15.7713347001544));
#178788=CARTESIAN_POINT('Ctrl Pts',(17.0284457747782,-17.6978921339815,
15.7718005722054));
#178789=CARTESIAN_POINT('Ctrl Pts',(17.0305638546939,-17.695016685123,15.772016563221));
#178790=CARTESIAN_POINT('Ctrl Pts',(17.0354125014323,-17.6884690546978,
15.772508148056));
#178791=CARTESIAN_POINT('Ctrl Pts',(17.0381476990232,-17.6848003652934,
15.7727834144827));
#178792=CARTESIAN_POINT('Ctrl Pts',(17.0465812188346,-17.6735647907638,
15.7736260010112));
#178793=CARTESIAN_POINT('Ctrl Pts',(17.0523185392419,-17.6660271389598,
15.7741906645266));
#178794=CARTESIAN_POINT('Ctrl Pts',(17.1322503964098,-17.5624630114758,
15.7819443981977));
#178795=CARTESIAN_POINT('Ctrl Pts',(17.2145286866137,-17.472935972836,15.7886001887928));
#178796=CARTESIAN_POINT('Ctrl Pts',(17.3839443253859,-17.3177474013176,
15.8011019253958));
#178797=CARTESIAN_POINT('Ctrl Pts',(17.4693525423884,-17.2507952223934,
15.8069418417311));
#178798=CARTESIAN_POINT('Ctrl Pts',(17.6043744854454,-17.1607592486249,
15.815974350041));
#178799=CARTESIAN_POINT('Ctrl Pts',(17.6503661690858,-17.1325675768534,
15.819017893463));
#178800=CARTESIAN_POINT('Ctrl Pts',(17.7169507811347,-17.0951737790149,
15.8234134095805));
#178801=CARTESIAN_POINT('Ctrl Pts',(17.7366928450442,-17.084496020637,15.8247152664774));
#178802=CARTESIAN_POINT('Ctrl Pts',(17.7717696322091,-17.066239103077,15.827028240413));
#178803=CARTESIAN_POINT('Ctrl Pts',(17.787033602579,-17.0585280414747,15.8280347113196));
#178804=CARTESIAN_POINT('Ctrl Pts',(17.8097464193935,-17.047397298406,15.8295329891039));
#178805=CARTESIAN_POINT('Ctrl Pts',(17.8171246364199,-17.0438344681445,
15.8300198003622));
#178806=CARTESIAN_POINT('Ctrl Pts',(17.8300552996081,-17.037682756556,15.8308732092417));
#178807=CARTESIAN_POINT('Ctrl Pts',(17.8355986797496,-17.0350749632634,
15.8312391455504));
#178808=CARTESIAN_POINT('Ctrl Pts',(17.8466659908122,-17.0299270769396,
15.8319699261856));
#178809=CARTESIAN_POINT('Ctrl Pts',(17.8521897007478,-17.0273866465295,
15.8323347544759));
#178810=CARTESIAN_POINT('Ctrl Pts',(17.8654310342758,-17.0213657449341,
15.8332095758929));
#178811=CARTESIAN_POINT('Ctrl Pts',(17.8731586980037,-17.0179077259414,
15.833720335174));
#178812=CARTESIAN_POINT('Ctrl Pts',(17.9011813969711,-17.0055691831373,
15.8355733863613));
#178813=CARTESIAN_POINT('Ctrl Pts',(17.9215942224466,-16.9969612422103,
15.8369249270421));
#178814=CARTESIAN_POINT('Ctrl Pts',(18.1138494702251,-16.919419468248,15.8496742686148));
#178815=CARTESIAN_POINT('Ctrl Pts',(18.2938744716083,-16.8730020674608,
15.8618670521711));
#178816=CARTESIAN_POINT('Ctrl Pts',(18.5574429208237,-16.8408420172486,
15.8793982076665));
#178817=CARTESIAN_POINT('Ctrl Pts',(18.6377919029663,-16.8356573626097,
15.8846844324742));
#178818=CARTESIAN_POINT('Ctrl Pts',(18.7543545483081,-16.8347898969838,
15.8921155935479));
#178819=CARTESIAN_POINT('Ctrl Pts',(18.7904670296205,-16.8354450720657,
15.8943844030806));
#178820=CARTESIAN_POINT('Ctrl Pts',(18.8340114125223,-16.8373504935855,
15.8970659420626));
#178821=CARTESIAN_POINT('Ctrl Pts',(18.8414737359984,-16.8377166184473,
15.897523558883));
#178822=CARTESIAN_POINT('Ctrl Pts',(18.8530883143883,-16.8383481171297,
15.8982326436105));
#178823=CARTESIAN_POINT('Ctrl Pts',(18.8572419037747,-16.8385862349207,
15.8984855952612));
#178824=CARTESIAN_POINT('Ctrl Pts',(18.8649540831465,-16.839051173689,15.8989540587022));
#178825=CARTESIAN_POINT('Ctrl Pts',(18.8685127684244,-16.8392747386586,
15.8991697446558));
#178826=CARTESIAN_POINT('Ctrl Pts',(18.8765702921974,-16.8398013724336,
15.8996570230034));
#178827=CARTESIAN_POINT('Ctrl Pts',(18.8810687257854,-16.8401098226303,
15.8999283105961));
#178828=CARTESIAN_POINT('Ctrl Pts',(18.892678665158,-16.8409431724365,15.9006266019916));
#178829=CARTESIAN_POINT('Ctrl Pts',(18.8997886321025,-16.8414896397551,
15.901052425327));
#178830=CARTESIAN_POINT('Ctrl Pts',(18.9433826825752,-16.8450619081063,
15.9036529345329));
#178831=CARTESIAN_POINT('Ctrl Pts',(18.9797883547807,-16.8489979368472,
15.9057800223777));
#178832=CARTESIAN_POINT('Ctrl Pts',(19.185121235868,-16.876603307102,15.917615682844));
#178833=CARTESIAN_POINT('Ctrl Pts',(19.3508153104973,-16.9196779860824,
15.9265900374109));
#178834=CARTESIAN_POINT('Ctrl Pts',(19.5983240232338,-17.0171268399761,
15.9412221850858));
#178835=CARTESIAN_POINT('Ctrl Pts',(19.6846181101444,-17.0580326567271,
15.9465711712111));
#178836=CARTESIAN_POINT('Ctrl Pts',(19.7865220539972,-17.1150612543843,
15.9533710312598));
#178837=CARTESIAN_POINT('Ctrl Pts',(19.8050299233889,-17.1257904054752,
15.9546262694712));
#178838=CARTESIAN_POINT('Ctrl Pts',(19.8310970183237,-17.1414342566027,
15.9564245901129));
#178839=CARTESIAN_POINT('Ctrl Pts',(19.8387927267763,-17.1461198251769,
15.9569593294526));
#178840=CARTESIAN_POINT('Ctrl Pts',(19.8520109046996,-17.1542838902018,
15.9578845281662));
#178841=CARTESIAN_POINT('Ctrl Pts',(19.8575476708812,-17.1577390869102,
15.9582741262711));
#178842=CARTESIAN_POINT('Ctrl Pts',(19.8681139866999,-17.1644010393384,
15.9590216164507));
#178843=CARTESIAN_POINT('Ctrl Pts',(19.8731461410982,-17.167603562244,15.9593793489408));
#178844=CARTESIAN_POINT('Ctrl Pts',(19.8861869817092,-17.1759805538481,
15.9603109947769));
#178845=CARTESIAN_POINT('Ctrl Pts',(19.8941742976707,-17.1811878958225,
15.9608861314053));
#178846=CARTESIAN_POINT('Ctrl Pts',(19.9212431739136,-17.1990972391178,
15.9628508781781));
#178847=CARTESIAN_POINT('Ctrl Pts',(19.9401529739022,-17.2120547761967,
15.9642500715595));
#178848=CARTESIAN_POINT('Ctrl Pts',(20.1027579186037,-17.3274009560412,
15.9765203133115));
#178849=CARTESIAN_POINT('Ctrl Pts',(20.2333152106197,-17.4470580130278,
15.9881037093106));
#178850=CARTESIAN_POINT('Ctrl Pts',(20.4033972526729,-17.6472939897339,
16.005461150955));
#178851=CARTESIAN_POINT('Ctrl Pts',(20.4552225885771,-17.7164678633397,
16.0111503512296));
#178852=CARTESIAN_POINT('Ctrl Pts',(20.523373185568,-17.8200766578057,16.0190669076583));
#178853=CARTESIAN_POINT('Ctrl Pts',(20.5432243806693,-17.8520843690389,
16.0214352013854));
#178854=CARTESIAN_POINT('Ctrl Pts',(20.5660252556376,-17.8911373096204,
16.0242179034205));
#178855=CARTESIAN_POINT('Ctrl Pts',(20.5698031132852,-17.8976883201116,
16.0246811579534));
#178856=CARTESIAN_POINT('Ctrl Pts',(20.5756146825765,-17.9078918472713,
16.0253970579462));
#178857=CARTESIAN_POINT('Ctrl Pts',(20.5776727713038,-17.9115303047537,
16.025651232608));
#178858=CARTESIAN_POINT('Ctrl Pts',(20.5814655527914,-17.9182820826468,
16.0261208154473));
#178859=CARTESIAN_POINT('Ctrl Pts',(20.583203145719,-17.9213936602332,16.0263364050088));
#178860=CARTESIAN_POINT('Ctrl Pts',(20.5871085834648,-17.9284289608655,
16.0268220199729));
#178861=CARTESIAN_POINT('Ctrl Pts',(20.5892718222449,-17.9323551791434,
16.0270917494463));
#178862=CARTESIAN_POINT('Ctrl Pts',(20.5956052439299,-17.9439370486092,
16.0278837453882));
#178863=CARTESIAN_POINT('Ctrl Pts',(20.59974068688,-17.951611728663,16.0284038488457));
#178864=CARTESIAN_POINT('Ctrl Pts',(20.6288254360826,-18.00639580176,16.0320846675931));
#178865=CARTESIAN_POINT('Ctrl Pts',(20.6520371413981,-18.0544114111279,
16.03514414567));
#178866=CARTESIAN_POINT('Ctrl Pts',(20.6801852874549,-18.1187310408185,
16.039092696787));
#178867=CARTESIAN_POINT('Ctrl Pts',(20.6867721725102,-18.134286605865,16.0400364071153));
#178868=CARTESIAN_POINT('Ctrl Pts',(20.7495007617665,-18.2875082992728,
16.0492372743885));
#178869=CARTESIAN_POINT('Ctrl Pts',(20.7911801703704,-18.4306500657084,
16.0571187250839));
#178870=CARTESIAN_POINT('Ctrl Pts',(20.8284373449654,-18.6376433294357,
16.0687552454186));
#178871=CARTESIAN_POINT('Ctrl Pts',(20.8367007241814,-18.698747715629,16.0722142940749));
#178872=CARTESIAN_POINT('Ctrl Pts',(20.8456567395971,-18.7971534085797,
16.0778852771615));
#178873=CARTESIAN_POINT('Ctrl Pts',(20.8480505818683,-18.8342649508023,
16.0800463668223));
#178874=CARTESIAN_POINT('Ctrl Pts',(20.8498893595605,-18.8825375860425,
16.0828940127973));
#178875=CARTESIAN_POINT('Ctrl Pts',(20.8502252205033,-18.8936594668152,
16.0835526097752));
#178876=CARTESIAN_POINT('Ctrl Pts',(20.8506288006009,-18.911749822692,16.0846281253856));
#178877=CARTESIAN_POINT('Ctrl Pts',(20.8507498188059,-18.918716984696,16.0850433696457));
#178878=CARTESIAN_POINT('Ctrl Pts',(20.8509163824109,-18.9321155,16.0858439534821));
#178879=CARTESIAN_POINT('Ctrl Pts',(20.8509670217873,-18.9385467212361,
16.0862291288333));
#178880=CARTESIAN_POINT('Ctrl Pts',(20.8510158621944,-18.9532711374946,
16.0871130964528));
#178881=CARTESIAN_POINT('Ctrl Pts',(20.8509946383011,-18.9615642522578,
16.0876124921698));
#178882=CARTESIAN_POINT('Ctrl Pts',(20.8508088196149,-18.9835928991429,
16.0889431612529));
#178883=CARTESIAN_POINT('Ctrl Pts',(20.8505592658744,-18.9973271459202,
16.08977708036));
#178884=CARTESIAN_POINT('Ctrl Pts',(20.8476429745416,-19.1018246375468,
16.0961555521935));
#178885=CARTESIAN_POINT('Ctrl Pts',(20.8392732291846,-19.1923224709446,
16.1018785383048));
#178886=CARTESIAN_POINT('Ctrl Pts',(20.8032181634376,-19.4207978880447,
16.1168162314853));
#178887=CARTESIAN_POINT('Ctrl Pts',(20.7675482784219,-19.5570716755587,
16.1262081025575));
#178888=CARTESIAN_POINT('Ctrl Pts',(20.6997977488651,-19.739566946158,16.13894990623));
#178889=CARTESIAN_POINT('Ctrl Pts',(20.6790045776565,-19.7896040096614,
16.1424575174684));
#178890=CARTESIAN_POINT('Ctrl Pts',(20.6445449312534,-19.8643027986768,
16.1476622344254));
#178891=CARTESIAN_POINT('Ctrl Pts',(20.6322688247292,-19.8895787848243,
16.1494175510262));
#178892=CARTESIAN_POINT('Ctrl Pts',(20.6163493386294,-19.9207609362137,
16.1515689305592));
#178893=CARTESIAN_POINT('Ctrl Pts',(20.6131759743504,-19.9269022744061,
16.1519919527315));
#178894=CARTESIAN_POINT('Ctrl Pts',(20.6081015785714,-19.9366057961958,
16.1526591092862));
#178895=CARTESIAN_POINT('Ctrl Pts',(20.6062203725,-19.9401782117273,16.1529044612158));
#178896=CARTESIAN_POINT('Ctrl Pts',(20.6026495583884,-19.9469123976665,
16.1533664272689));
#178897=CARTESIAN_POINT('Ctrl Pts',(20.6009621605159,-19.9500752188442,
16.1535831695517));
#178898=CARTESIAN_POINT('Ctrl Pts',(20.5970812099536,-19.957305306156,16.1540781339038));
#178899=CARTESIAN_POINT('Ctrl Pts',(20.5948823710689,-19.9613696822472,
16.1543560161919));
#178900=CARTESIAN_POINT('Ctrl Pts',(20.5889996413363,-19.9721588717554,
16.1550928017429));
#178901=CARTESIAN_POINT('Ctrl Pts',(20.5852924546031,-19.9788709970271,
16.1555502615088));
#178902=CARTESIAN_POINT('Ctrl Pts',(20.5587909112841,-20.0262439172689,
16.158773553888));
#178903=CARTESIAN_POINT('Ctrl Pts',(20.5346936962701,-20.0661655092835,
16.1614617893916));
#178904=CARTESIAN_POINT('Ctrl Pts',(20.5068125481072,-20.1090848941097,
16.1643570633199));
#178905=CARTESIAN_POINT('Ctrl Pts',(20.5043167135478,-20.1128998738619,
16.1646144609876));
#178906=CARTESIAN_POINT('Ctrl Pts',(20.4889698185111,-20.1361936099222,
16.1661865588864));
#178907=CARTESIAN_POINT('Ctrl Pts',(20.4758094094793,-20.1554673266876,
16.167489344523));
#178908=CARTESIAN_POINT('Ctrl Pts',(20.436056947628,-20.2116672095203,16.1713059271141));
#178909=CARTESIAN_POINT('Ctrl Pts',(20.4085896483035,-20.2479587472541,
16.1737939101594));
#178910=CARTESIAN_POINT('Ctrl Pts',(20.3112066886066,-20.3683562640255,
16.1822246657831));
#178911=CARTESIAN_POINT('Ctrl Pts',(20.2359567760231,-20.4479181008005,
16.1881126735045));
#178912=CARTESIAN_POINT('Ctrl Pts',(20.1140502965276,-20.5582960729378,
16.1972568180917));
#178913=CARTESIAN_POINT('Ctrl Pts',(20.0717731692527,-20.593672378155,16.2003642246821));
#178914=CARTESIAN_POINT('Ctrl Pts',(20.0010165044206,-20.6483298996806,
16.2055080701845));
#178915=CARTESIAN_POINT('Ctrl Pts',(19.9733622000711,-20.6686383112002,
16.2075051247608));
#178916=CARTESIAN_POINT('Ctrl Pts',(19.9363628901784,-20.6944492275682,
16.2101657063372));
#178917=CARTESIAN_POINT('Ctrl Pts',(19.9274509035291,-20.7005653446864,
16.2108057064886));
#178918=CARTESIAN_POINT('Ctrl Pts',(19.9127752657263,-20.7104724784298,
16.2118584056923));
#178919=CARTESIAN_POINT('Ctrl Pts',(19.9070391598751,-20.7143040918499,
16.2122695635035));
#178920=CARTESIAN_POINT('Ctrl Pts',(19.8958978603225,-20.7216677803985,
16.213067631105));
#178921=CARTESIAN_POINT('Ctrl Pts',(19.8904950265313,-20.7252032999569,
16.2134544055281));
#178922=CARTESIAN_POINT('Ctrl Pts',(19.8779803863855,-20.733311134783,16.2143497891331));
#178923=CARTESIAN_POINT('Ctrl Pts',(19.8708572297515,-20.7378656498345,
16.2148590544676));
#178924=CARTESIAN_POINT('Ctrl Pts',(19.8516216643262,-20.7500030656846,
16.2162333841592));
#178925=CARTESIAN_POINT('Ctrl Pts',(19.8394596045894,-20.7575060940593,
16.2171013767246));
#178926=CARTESIAN_POINT('Ctrl Pts',(19.727145564418,-20.825234739053,16.2251096917076));
#178927=CARTESIAN_POINT('Ctrl Pts',(19.6222596816702,-20.8771839983641,
16.2325518830783));
#178928=CARTESIAN_POINT('Ctrl Pts',(19.3623085969813,-20.9801547196364,
16.2508154736745));
#178929=CARTESIAN_POINT('Ctrl Pts',(19.2045739197855,-21.0224452483299,
16.2617770490455));
#178930=CARTESIAN_POINT('Ctrl Pts',(19.011448730543,-21.0509912763467,16.274181337372));
#178931=CARTESIAN_POINT('Ctrl Pts',(18.979237897354,-21.0549980545058,16.2762152488124));
#178932=CARTESIAN_POINT('Ctrl Pts',(18.939746573596,-21.0589906750871,16.2786560395557));
#178933=CARTESIAN_POINT('Ctrl Pts',(18.9325436234497,-21.0596816150739,
16.2790990792166));
#178934=CARTESIAN_POINT('Ctrl Pts',(18.9212451285424,-21.0607069840108,
16.2797905178954));
#178935=CARTESIAN_POINT('Ctrl Pts',(18.9171519907479,-21.0610664360155,
16.2800402858223));
#178936=CARTESIAN_POINT('Ctrl Pts',(18.9094985884157,-21.0617160957521,
16.2805059236637));
#178937=CARTESIAN_POINT('Ctrl Pts',(18.9059386752022,-21.0620092064753,
16.2807219487286));
#178938=CARTESIAN_POINT('Ctrl Pts',(18.897809885945,-21.0626577935262,16.2812139588645));
#178939=CARTESIAN_POINT('Ctrl Pts',(18.8932405956802,-21.0630074452023,
16.2814896143374));
#178940=CARTESIAN_POINT('Ctrl Pts',(18.8791897186696,-21.0640367673506,
16.2823345769834));
#178941=CARTESIAN_POINT('Ctrl Pts',(18.8697045101551,-21.0646674264054,
16.2829012057517));
#178942=CARTESIAN_POINT('Ctrl Pts',(18.7843093456043,-21.0697677441233,
16.2879711841856));
#178943=CARTESIAN_POINT('Ctrl Pts',(18.7082054014633,-21.070208796356,16.2922673244558));
#178944=CARTESIAN_POINT('Ctrl Pts',(18.5898140850792,-21.0645110947877,
16.2988269208558));
#178945=CARTESIAN_POINT('Ctrl Pts',(18.547463081989,-21.0611934155097,16.3011484938636));
#178946=CARTESIAN_POINT('Ctrl Pts',(18.3965607709308,-21.0447910546901,
16.3094124856806));
#178947=CARTESIAN_POINT('Ctrl Pts',(18.2889612781282,-21.0245779311487,
16.3152990669983));
#178948=CARTESIAN_POINT('Ctrl Pts',(18.1302306184801,-20.9818237747983,
16.3244398954967));
#178949=CARTESIAN_POINT('Ctrl Pts',(18.0776353880004,-20.9654316165808,
16.327545401422));
#178950=CARTESIAN_POINT('Ctrl Pts',(17.9934267495775,-20.9355362666617,
16.3326863811211));
#178951=CARTESIAN_POINT('Ctrl Pts',(17.9613968965364,-20.9232810831048,
16.3346825280834));
#178952=CARTESIAN_POINT('Ctrl Pts',(17.9196834611983,-20.9061479896563,
16.3373420718212));
#178953=CARTESIAN_POINT('Ctrl Pts',(17.9097185865706,-20.9019656242518,
16.3379819651689));
#178954=CARTESIAN_POINT('Ctrl Pts',(17.8934466770621,-20.8949891122312,
16.3390345334454));
#178955=CARTESIAN_POINT('Ctrl Pts',(17.8871204257654,-20.89224007895,16.3394456678857));
#178956=CARTESIAN_POINT('Ctrl Pts',(17.8748983853308,-20.8868579039729,
16.3402437221114));
#178957=CARTESIAN_POINT('Ctrl Pts',(17.8690009795193,-20.8842286060475,
16.340630506699));
#178958=CARTESIAN_POINT('Ctrl Pts',(17.855408603304,-20.8780938859998,16.341525960443));
#178959=CARTESIAN_POINT('Ctrl Pts',(17.8477224607239,-20.8745692757786,
16.3420352860753));
#178960=CARTESIAN_POINT('Ctrl Pts',(17.827101021306,-20.8649630285519,16.3434098840022));
#178961=CARTESIAN_POINT('Ctrl Pts',(17.8142060342502,-20.8587963580319,
16.3442780862837));
#178962=CARTESIAN_POINT('Ctrl Pts',(17.6962262732674,-20.8009005808381,
16.3523026058879));
#178963=CARTESIAN_POINT('Ctrl Pts',(17.5955586507501,-20.7406729997485,
16.3597622111443));
#178964=CARTESIAN_POINT('Ctrl Pts',(17.3674340186021,-20.5771018086952,
16.3780996966685));
#178965=CARTESIAN_POINT('Ctrl Pts',(17.2459722416748,-20.4666722654724,
16.3891199719299));
#178966=CARTESIAN_POINT('Ctrl Pts',(17.1177574528905,-20.3196400550649,
16.4015037911325));
#178967=CARTESIAN_POINT('Ctrl Pts',(17.0976052224759,-20.2954625668438,
16.403474683421));
#178968=CARTESIAN_POINT('Ctrl Pts',(17.0735333296601,-20.2652367671559,
16.4058503994211));
#178969=CARTESIAN_POINT('Ctrl Pts',(17.0690967018619,-20.2596075027145,
16.4062891921075));
#178970=CARTESIAN_POINT('Ctrl Pts',(17.0621710199215,-20.2507276928364,
16.406975483563));
#178971=CARTESIAN_POINT('Ctrl Pts',(17.0596627075544,-20.2474923351964,
16.4072243185171));
#178972=CARTESIAN_POINT('Ctrl Pts',(17.0549819727073,-20.2414185664612,
16.4076891548603));
#178973=CARTESIAN_POINT('Ctrl Pts',(17.0528073784729,-20.2385819620404,
16.4079053057623));
#178974=CARTESIAN_POINT('Ctrl Pts',(17.0478470215855,-20.2320774766881,
16.4083988232835));
#178975=CARTESIAN_POINT('Ctrl Pts',(17.0450660427117,-20.2284060097705,
16.4086758525205));
#178976=CARTESIAN_POINT('Ctrl Pts',(17.0378179745889,-20.2187718987769,
16.4093988612888));
#178977=CARTESIAN_POINT('Ctrl Pts',(17.0333702961248,-20.2127946386531,
16.409843516853));
#178978=CARTESIAN_POINT('Ctrl Pts',(17.0039151561351,-20.1727702473765,
16.4127958625758));
#178979=CARTESIAN_POINT('Ctrl Pts',(16.9798982063689,-20.1380021079905,
16.4152399444127));
#178980=CARTESIAN_POINT('Ctrl Pts',(16.9164802357213,-20.0400496880174,
16.4218683513697));
#178981=CARTESIAN_POINT('Ctrl Pts',(16.8793454306222,-19.9754686764816,
16.4259561035331));
#178982=CARTESIAN_POINT('Ctrl Pts',(16.7951472797133,-19.8093431575168,
16.4361043561752));
#178983=CARTESIAN_POINT('Ctrl Pts',(16.7525863070628,-19.7057812498675,
16.4421169529417));
#178984=CARTESIAN_POINT('Ctrl Pts',(16.6925866262591,-19.518963755382,16.4530200327051));
#178985=CARTESIAN_POINT('Ctrl Pts',(16.6716050219941,-19.4371195556745,
16.457812439815));
#178986=CARTESIAN_POINT('Ctrl Pts',(16.6528673353179,-19.3403009414751,
16.4636013834646));
#178987=CARTESIAN_POINT('Ctrl Pts',(16.650308712979,-19.3263279241678,16.4644395951184));
#178988=CARTESIAN_POINT('Ctrl Pts',(16.6465902583539,-19.30480018066,16.4657356113839));
#178989=CARTESIAN_POINT('Ctrl Pts',(16.6453303598907,-19.2972629854671,
16.4661902323967));
#178990=CARTESIAN_POINT('Ctrl Pts',(16.6431068637625,-19.2835034500645,
16.4670218085244));
#178991=CARTESIAN_POINT('Ctrl Pts',(16.6421301613061,-19.2772832937722,
16.4673983427374));
#178992=CARTESIAN_POINT('Ctrl Pts',(16.6400580229959,-19.2636914158526,
16.4682224921851));
#178993=CARTESIAN_POINT('Ctrl Pts',(16.6389737394915,-19.2563181022256,
16.4686704557581));
#178994=CARTESIAN_POINT('Ctrl Pts',(16.6361094461845,-19.2360992763592,
16.4699013252763));
#178995=CARTESIAN_POINT('Ctrl Pts',(16.6344085230222,-19.2232430509384,
16.4706867196878));
#178996=CARTESIAN_POINT('Ctrl Pts',(16.6263685201593,-19.1578589105123,
16.4746955627278));
#178997=CARTESIAN_POINT('Ctrl Pts',(16.6218825847585,-19.105126054127,16.4779768409725));
#178998=CARTESIAN_POINT('Ctrl Pts',(16.617766361128,-19.0183299141281,16.4834601044147));
#178999=CARTESIAN_POINT('Ctrl Pts',(16.6169742106524,-18.9843434164516,
16.4856276621907));
#179000=CARTESIAN_POINT('Ctrl Pts',(16.6171022081763,-18.8197312259874,
16.4962188776041));
#179001=CARTESIAN_POINT('Ctrl Pts',(16.6292932871456,-18.6894054728747,
16.5049104190834));
#179002=CARTESIAN_POINT('Ctrl Pts',(16.6709615320031,-18.4676530475529,
16.5197603279542));
#179003=CARTESIAN_POINT('Ctrl Pts',(16.6947819253757,-18.375533519513,16.5259401150738));
#179004=CARTESIAN_POINT('Ctrl Pts',(16.7277657538437,-18.276125045736,16.5324111806187));
#179005=CARTESIAN_POINT('Ctrl Pts',(16.7308789356263,-18.2669534220978,
16.5330062673888));
#179006=CARTESIAN_POINT('Ctrl Pts',(16.7355692054842,-18.253440996125,16.5338797814061));
#179007=CARTESIAN_POINT('Ctrl Pts',(16.7370976771306,-18.2490836207518,
16.5341609683186));
#179008=CARTESIAN_POINT('Ctrl Pts',(16.7398349366889,-18.241361213979,16.5346583782767));
#179009=CARTESIAN_POINT('Ctrl Pts',(16.7410380033782,-18.2379942124689,
16.5348749355805));
#179010=CARTESIAN_POINT('Ctrl Pts',(16.7432997980327,-18.2317144243437,
16.5352782381891));
#179011=CARTESIAN_POINT('Ctrl Pts',(16.7443563829228,-18.2288009389497,
16.5354651111096));
#179012=CARTESIAN_POINT('Ctrl Pts',(16.7454193692319,-18.2258897639242,
16.5356516076535));
#179013=CARTESIAN_POINT('Origin',(18.734,-18.952,0.));
#179014=CARTESIAN_POINT('',(16.7454193574352,-18.2258897962317,17.5536949220328));
#179015=CARTESIAN_POINT('',(16.7454193703768,-18.2258897607889,17.3329785739071));
#179016=CARTESIAN_POINT('',(16.7454193692319,-18.2258897639242,0.));
#179017=CARTESIAN_POINT('',(16.6170009798014,-18.9502127592998,17.5117108725788));
#179018=CARTESIAN_POINT('Ctrl Pts',(16.7454193574352,-18.2258897962317,
17.5536949220328));
#179019=CARTESIAN_POINT('Ctrl Pts',(16.7413714151833,-18.2369757988282,
17.5529503472539));
#179020=CARTESIAN_POINT('Ctrl Pts',(16.7374153734205,-18.2480978513274,
17.5522096669621));
#179021=CARTESIAN_POINT('Ctrl Pts',(16.7284957195804,-18.2738552394198,
17.5505098130367));
#179022=CARTESIAN_POINT('Ctrl Pts',(16.7235995003856,-18.2885110414992,
17.5495540496509));
#179023=CARTESIAN_POINT('Ctrl Pts',(16.7171006505231,-18.3086967106174,
17.5482545722139));
#179024=CARTESIAN_POINT('Ctrl Pts',(16.7153595931654,-18.3141810462808,
17.5479032140515));
#179025=CARTESIAN_POINT('Ctrl Pts',(16.7126241636862,-18.322921057949,17.5473460619894));
#179026=CARTESIAN_POINT('Ctrl Pts',(16.7116152609576,-18.3261721046219,
17.547139427821));
#179027=CARTESIAN_POINT('Ctrl Pts',(16.7095441547532,-18.3329032629761,
17.5467128847844));
#179028=CARTESIAN_POINT('Ctrl Pts',(16.7084830809009,-18.336383683007,17.5464930479701));
#179029=CARTESIAN_POINT('Ctrl Pts',(16.7059703217907,-18.3447025915504,
17.5459692588079));
#179030=CARTESIAN_POINT('Ctrl Pts',(16.7045269600696,-18.3495436120295,
17.545665792097));
#179031=CARTESIAN_POINT('Ctrl Pts',(16.6996912337203,-18.3659771875174,
17.5446400284771));
#179032=CARTESIAN_POINT('Ctrl Pts',(16.6963806855563,-18.3775938388039,
17.5439223413945));
#179033=CARTESIAN_POINT('Ctrl Pts',(16.6886497495818,-18.4056297446831,
17.5422066455205));
#179034=CARTESIAN_POINT('Ctrl Pts',(16.6843273312696,-18.4220753909503,
17.541213684684));
#179035=CARTESIAN_POINT('Ctrl Pts',(16.668771959161,-18.4842994252448,17.5375011482999));
#179036=CARTESIAN_POINT('Ctrl Pts',(16.6588701449653,-18.5303990672132,
17.5348407975409));
#179037=CARTESIAN_POINT('Ctrl Pts',(16.6283221116876,-18.7000293569035,
17.525255197217));
#179038=CARTESIAN_POINT('Ctrl Pts',(16.6171065838711,-18.8249907791413,
17.5185706197638));
#179039=CARTESIAN_POINT('Ctrl Pts',(16.6170007560361,-18.95021085035,17.5117113679171));
#179040=CARTESIAN_POINT('Ctrl Pts',(16.6170007544058,-18.9502127804554,
17.5117112621906));
#179041=CARTESIAN_POINT('Ctrl Pts',(16.6169304738018,-19.0334616382956,
17.5071510906457));
#179042=CARTESIAN_POINT('Ctrl Pts',(16.6217706589722,-19.1166375130435,
17.5025270065186));
#179043=CARTESIAN_POINT('Ctrl Pts',(16.6354867191127,-19.233244553671,17.4958023784479));
#179044=CARTESIAN_POINT('Ctrl Pts',(16.640299115908,-19.2670760339661,17.4938228290134));
#179045=CARTESIAN_POINT('Ctrl Pts',(16.6476157596072,-19.3108798684298,
17.491216464112));
#179046=CARTESIAN_POINT('Ctrl Pts',(16.6493769145509,-19.3209722816618,
17.4906129592889));
#179047=CARTESIAN_POINT('Ctrl Pts',(16.6524780889849,-19.3380124286009,
17.4895887495204));
#179048=CARTESIAN_POINT('Ctrl Pts',(16.6537798228097,-19.3449670134176,
17.4891692578465));
#179049=CARTESIAN_POINT('Ctrl Pts',(16.6564245658922,-19.358715221747,17.4883369899524));
#179050=CARTESIAN_POINT('Ctrl Pts',(16.6577660954574,-19.3655090420839,
17.4879242654479));
#179051=CARTESIAN_POINT('Ctrl Pts',(16.6604207587197,-19.3786142129694,
17.4871252735954));
#179052=CARTESIAN_POINT('Ctrl Pts',(16.6617294358375,-19.3849263956566,
17.4867391528484));
#179053=CARTESIAN_POINT('Ctrl Pts',(16.6648077221552,-19.3994401798843,
17.4858483391349));
#179054=CARTESIAN_POINT('Ctrl Pts',(16.6665972917148,-19.4076373951692,
17.4853430110984));
#179055=CARTESIAN_POINT('Ctrl Pts',(16.6715178229252,-19.429550193613,17.4839861569912));
#179056=CARTESIAN_POINT('Ctrl Pts',(16.6747368134473,-19.4432453884597,
17.4831318174468));
#179057=CARTESIAN_POINT('Ctrl Pts',(16.7030023345249,-19.5583384343218,
17.4758975009352));
#179058=CARTESIAN_POINT('Ctrl Pts',(16.7353809208197,-19.6577718654768,
17.4692788495735));
#179059=CARTESIAN_POINT('Ctrl Pts',(16.8068986778427,-19.8323811165516,
17.4570149658523));
#179060=CARTESIAN_POINT('Ctrl Pts',(16.8434657138016,-19.9083834675659,
17.45144184036));
#179061=CARTESIAN_POINT('Ctrl Pts',(16.9296233906247,-20.0630939097261,
17.4397430179211));
#179062=CARTESIAN_POINT('Ctrl Pts',(16.9800719491005,-20.1411356371382,
17.4336307215776));
#179063=CARTESIAN_POINT('Ctrl Pts',(17.0539803422169,-20.2404809713889,
17.4257741628426));
#179064=CARTESIAN_POINT('Ctrl Pts',(17.0730217096313,-20.2649358772608,
17.4238340413425));
#179065=CARTESIAN_POINT('Ctrl Pts',(17.0970989611475,-20.2944957605528,
17.4214901795506));
#179066=CARTESIAN_POINT('Ctrl Pts',(17.1016316456187,-20.3000035003857,
17.4210535170314));
#179067=CARTESIAN_POINT('Ctrl Pts',(17.1088046138549,-20.3086302567729,
17.4203698082325));
#179068=CARTESIAN_POINT('Ctrl Pts',(17.1114261896776,-20.3117646588463,
17.4201214420577));
#179069=CARTESIAN_POINT('Ctrl Pts',(17.116358709412,-20.3176274892084,17.4196570034692));
#179070=CARTESIAN_POINT('Ctrl Pts',(17.118667463459,-20.3203576217125,17.4194407843878));
#179071=CARTESIAN_POINT('Ctrl Pts',(17.1239738343295,-20.3266003305954,
17.4189464868741));
#179072=CARTESIAN_POINT('Ctrl Pts',(17.1269760293182,-20.3301089512796,
17.4186687498332));
#179073=CARTESIAN_POINT('Ctrl Pts',(17.1363107954761,-20.3409463693886,
17.4178110092996));
#179074=CARTESIAN_POINT('Ctrl Pts',(17.1426823022761,-20.3482416711482,
17.4172338030958));
#179075=CARTESIAN_POINT('Ctrl Pts',(17.2191980624413,-20.4346471793953,
17.4103960435262));
#179076=CARTESIAN_POINT('Ctrl Pts',(17.2951338106021,-20.5084503707135,
17.4045386166813));
#179077=CARTESIAN_POINT('Ctrl Pts',(17.5054690018733,-20.6842682445332,
17.3895655348813));
#179078=CARTESIAN_POINT('Ctrl Pts',(17.6470724835729,-20.7764526196379,
17.3805829394062));
#179079=CARTESIAN_POINT('Ctrl Pts',(17.822655576485,-20.8629918486194,17.3693878594998));
#179080=CARTESIAN_POINT('Ctrl Pts',(17.8474436531446,-20.8746170320157,
17.36780778385));
#179081=CARTESIAN_POINT('Ctrl Pts',(17.890732859955,-20.8939037486668,17.3650446455047));
#179082=CARTESIAN_POINT('Ctrl Pts',(17.9091304099634,-20.9017896700504,
17.3638692028871));
#179083=CARTESIAN_POINT('Ctrl Pts',(17.9357223705074,-20.9127443234659,
17.3621674562089));
#179084=CARTESIAN_POINT('Ctrl Pts',(17.94382864892,-20.916025129215,17.3616483353886));
#179085=CARTESIAN_POINT('Ctrl Pts',(17.9580051965668,-20.9216607463205,
17.3607397532174));
#179086=CARTESIAN_POINT('Ctrl Pts',(17.9640664729106,-20.9240379694504,
17.3603510531793));
#179087=CARTESIAN_POINT('Ctrl Pts',(17.9757188816356,-20.9285461154423,
17.3596033232956));
#179088=CARTESIAN_POINT('Ctrl Pts',(17.9813082786803,-20.9306813721396,
17.3592444435844));
#179089=CARTESIAN_POINT('Ctrl Pts',(17.9959234141704,-20.9361937461023,
17.3583054597131));
#179090=CARTESIAN_POINT('Ctrl Pts',(18.0049632171588,-20.9395329514456,
17.3577240938987));
#179091=CARTESIAN_POINT('Ctrl Pts',(18.036161112823,-20.9508156402387,17.3557155218438));
#179092=CARTESIAN_POINT('Ctrl Pts',(18.0584280752299,-20.9584509912777,
17.354278145317));
#179093=CARTESIAN_POINT('Ctrl Pts',(18.2402544669451,-21.017429548226,17.3425060558339));
#179094=CARTESIAN_POINT('Ctrl Pts',(18.4052411676596,-21.0500183426998,
17.3315368351925));
#179095=CARTESIAN_POINT('Ctrl Pts',(18.6971294514733,-21.0723777872687,
17.3121910022218));
#179096=CARTESIAN_POINT('Ctrl Pts',(18.8225689067809,-21.0708495821324,
17.3039194491839));
#179097=CARTESIAN_POINT('Ctrl Pts',(18.9590204336079,-21.0570409003437,
17.2954142426233));
#179098=CARTESIAN_POINT('Ctrl Pts',(18.9708823738012,-21.055739086411,17.2946791143928));
#179099=CARTESIAN_POINT('Ctrl Pts',(18.9877249183501,-21.0537464009877,
17.2936419606708));
#179100=CARTESIAN_POINT('Ctrl Pts',(18.9927147954818,-21.0531380069029,
17.2933355170668));
#179101=CARTESIAN_POINT('Ctrl Pts',(19.0013083959076,-21.0520591488736,
17.2928092441102));
#179102=CARTESIAN_POINT('Ctrl Pts',(19.0049131460946,-21.0515971697787,
17.2925889405603));
#179103=CARTESIAN_POINT('Ctrl Pts',(19.011898612675,-21.0506836335322,17.2921629209678));
#179104=CARTESIAN_POINT('Ctrl Pts',(19.0152794271839,-21.05023318933,17.2919571409472));
#179105=CARTESIAN_POINT('Ctrl Pts',(19.0243947358565,-21.0489962803707,
17.2914033745344));
#179106=CARTESIAN_POINT('Ctrl Pts',(19.0301271663692,-21.0481944579716,
17.2910562491542));
#179107=CARTESIAN_POINT('Ctrl Pts',(19.0513721364507,-21.0451339335721,
17.289773709563));
#179108=CARTESIAN_POINT('Ctrl Pts',(19.0668631684812,-21.0427264001738,
17.2888463317429));
#179109=CARTESIAN_POINT('Ctrl Pts',(19.2155428960719,-21.0179249394503,
17.280008389634));
#179110=CARTESIAN_POINT('Ctrl Pts',(19.3463463229008,-20.9830025742286,
17.2727063784694));
#179111=CARTESIAN_POINT('Ctrl Pts',(19.6191655652255,-20.8813828491795,
17.2568966641222));
#179112=CARTESIAN_POINT('Ctrl Pts',(19.7588984006038,-20.8109276533858,
17.2484018466449));
#179113=CARTESIAN_POINT('Ctrl Pts',(19.9074405477088,-20.7141517712137,
17.2380772478022));
#179114=CARTESIAN_POINT('Ctrl Pts',(19.9250887823573,-20.7022711355029,
17.2368288459338));
#179115=CARTESIAN_POINT('Ctrl Pts',(19.9499355347727,-20.6849946895212,
17.2350386370128));
#179116=CARTESIAN_POINT('Ctrl Pts',(19.9572837000914,-20.6798156162987,
17.2345050692874));
#179117=CARTESIAN_POINT('Ctrl Pts',(19.9699061409286,-20.6707982888845,
17.2335812578259));
#179118=CARTESIAN_POINT('Ctrl Pts',(19.9751961130677,-20.6669821440746,
17.233191868419));
#179119=CARTESIAN_POINT('Ctrl Pts',(19.9852929633915,-20.6596271690569,
17.2324443315621));
#179120=CARTESIAN_POINT('Ctrl Pts',(19.9901026833484,-20.6560923321479,
17.2320863415411));
#179121=CARTESIAN_POINT('Ctrl Pts',(20.0025749704088,-20.6468445053715,
17.2311530420332));
#179122=CARTESIAN_POINT('Ctrl Pts',(20.0102138480243,-20.6410999266948,
17.2305765006436));
#179123=CARTESIAN_POINT('Ctrl Pts',(20.0361512259079,-20.6213181420612,
17.2286018182644));
#179124=CARTESIAN_POINT('Ctrl Pts',(20.0542586234261,-20.6070341313103,
17.2271939621623));
#179125=CARTESIAN_POINT('Ctrl Pts',(20.2073751973753,-20.4821362645431,
17.2150307346349));
#179126=CARTESIAN_POINT('Ctrl Pts',(20.328435538637,-20.3555325794204,17.2035802962184));
#179127=CARTESIAN_POINT('Ctrl Pts',(20.4849024782737,-20.1451964155519,
17.1862589416547));
#179128=CARTESIAN_POINT('Ctrl Pts',(20.5328183961388,-20.0716568609642,
17.1804785067545));
#179129=CARTESIAN_POINT('Ctrl Pts',(20.5947618329447,-19.9622958974445,
17.1724528915946));
#179130=CARTESIAN_POINT('Ctrl Pts',(20.6125941671862,-19.9287378202598,
17.1700628187077));
#179131=CARTESIAN_POINT('Ctrl Pts',(20.6328908004931,-19.8879274571345,
17.1672580293692));
#179132=CARTESIAN_POINT('Ctrl Pts',(20.6362304114609,-19.8811210593469,
17.166793579358));
#179133=CARTESIAN_POINT('Ctrl Pts',(20.6413564020617,-19.8705303828504,
17.1660762348604));
#179134=CARTESIAN_POINT('Ctrl Pts',(20.6431682084479,-19.8667585808596,
17.1658218014577));
#179135=CARTESIAN_POINT('Ctrl Pts',(20.6465022958226,-19.8597646541829,
17.1653519795243));
#179136=CARTESIAN_POINT('Ctrl Pts',(20.6480276112758,-19.8565440854293,
17.1651364080874));
#179137=CARTESIAN_POINT('Ctrl Pts',(20.6514510223034,-19.8492684228995,
17.1646511347528));
#179138=CARTESIAN_POINT('Ctrl Pts',(20.6533443846704,-19.8452111617896,
17.1643817269502));
#179139=CARTESIAN_POINT('Ctrl Pts',(20.6588757726999,-19.8332592238418,
17.1635915503718));
#179140=CARTESIAN_POINT('Ctrl Pts',(20.6624781135022,-19.8253480013949,
17.1630729297659));
#179141=CARTESIAN_POINT('Ctrl Pts',(20.6876008168352,-19.7692617560708,
17.1594257598493));
#179142=CARTESIAN_POINT('Ctrl Pts',(20.7073641585449,-19.7203149204864,
17.1563963707161));
#179143=CARTESIAN_POINT('Ctrl Pts',(20.7307032603142,-19.6556479020907,
17.1525281198126));
#179144=CARTESIAN_POINT('Ctrl Pts',(20.735957063009,-19.6405580701476,17.1516347921442));
#179145=CARTESIAN_POINT('Ctrl Pts',(20.7571454890679,-19.5774078138515,
17.1479295510806));
#179146=CARTESIAN_POINT('Ctrl Pts',(20.7715246361901,-19.5288416622487,
17.1451596034167));
#179147=CARTESIAN_POINT('Ctrl Pts',(20.8114258098308,-19.3738539000839,
17.1364459819417));
#179148=CARTESIAN_POINT('Ctrl Pts',(20.8304479895602,-19.2659484962345,
17.1305551319957));
#179149=CARTESIAN_POINT('Ctrl Pts',(20.8463898655661,-19.1021421846975,
17.1214043793214));
#179150=CARTESIAN_POINT('Ctrl Pts',(20.8495851592457,-19.0470389728025,
17.118293184714));
#179151=CARTESIAN_POINT('Ctrl Pts',(20.8512712123662,-18.9575442512807,
17.1131436281628));
#179152=CARTESIAN_POINT('Ctrl Pts',(20.8510825804375,-18.9232028484331,
17.1111447653357));
#179153=CARTESIAN_POINT('Ctrl Pts',(20.8497365137264,-18.8780749468508,
17.1084821160901));
#179154=CARTESIAN_POINT('Ctrl Pts',(20.8493313558287,-18.8672700909863,
17.1078419032162));
#179155=CARTESIAN_POINT('Ctrl Pts',(20.8485321309317,-18.8495770398198,
17.1067889431909));
#179156=CARTESIAN_POINT('Ctrl Pts',(20.8481871265019,-18.842686744097,17.1063777387798));
#179157=CARTESIAN_POINT('Ctrl Pts',(20.8474540544223,-18.8293515327965,
17.1055796443721));
#179158=CARTESIAN_POINT('Ctrl Pts',(20.8470701697673,-18.8229064569063,
17.1051928900797));
#179159=CARTESIAN_POINT('Ctrl Pts',(20.8461156360282,-18.8080278144545,
17.1042976457736));
#179160=CARTESIAN_POINT('Ctrl Pts',(20.8455239500489,-18.7995957503937,
17.1037885002504));
#179161=CARTESIAN_POINT('Ctrl Pts',(20.8437966519874,-18.7769254371075,
17.1024147036412));
#179162=CARTESIAN_POINT('Ctrl Pts',(20.8425674281465,-18.7626949536508,
17.1015471278806));
#179163=CARTESIAN_POINT('Ctrl Pts',(20.8276355885117,-18.6080958002519,
17.0920634644556));
#179164=CARTESIAN_POINT('Ctrl Pts',(20.8000852563815,-18.4694459136423,
17.0829978303278));
#179165=CARTESIAN_POINT('Ctrl Pts',(20.7307945966785,-18.2421892491328,
17.0673675450501));
#179166=CARTESIAN_POINT('Ctrl Pts',(20.6963316889671,-18.1518284542033,
17.060942004802));
#179167=CARTESIAN_POINT('Ctrl Pts',(20.635269890882,-18.0196575505104,17.0514409668087));
#179168=CARTESIAN_POINT('Ctrl Pts',(20.6131815916944,-17.9759022483213,
17.0482790106928));
#179169=CARTESIAN_POINT('Ctrl Pts',(20.5769516840405,-17.9099310052912,
17.0435261713027));
#179170=CARTESIAN_POINT('Ctrl Pts',(20.563882076425,-17.8871476944359,17.0418876090633));
#179171=CARTESIAN_POINT('Ctrl Pts',(20.5469189535631,-17.8588122001037,
17.0398589504759));
#179172=CARTESIAN_POINT('Ctrl Pts',(20.5434188770552,-17.853028649946,17.0394453733763));
#179173=CARTESIAN_POINT('Ctrl Pts',(20.5378019121738,-17.8438467210566,
17.0387896907196));
#179174=CARTESIAN_POINT('Ctrl Pts',(20.535703017919,-17.8404374674221,17.0385464365064));
#179175=CARTESIAN_POINT('Ctrl Pts',(20.5317021285747,-17.8339798900203,
17.0380860939183));
#179176=CARTESIAN_POINT('Ctrl Pts',(20.5298020686265,-17.8309304928456,
17.0378688905139));
#179177=CARTESIAN_POINT('Ctrl Pts',(20.525408345417,-17.8239188607269,17.0373698538717));
#179178=CARTESIAN_POINT('Ctrl Pts',(20.5229092968791,-17.8199600513604,
17.0370883803241));
#179179=CARTESIAN_POINT('Ctrl Pts',(20.5161716320798,-17.8093647645656,
17.0363357253899));
#179180=CARTESIAN_POINT('Ctrl Pts',(20.511909039558,-17.8027435191116,17.0358660879167));
#179181=CARTESIAN_POINT('Ctrl Pts',(20.4795855399492,-17.7531444593571,
17.0323522518052));
#179182=CARTESIAN_POINT('Ctrl Pts',(20.4500044352946,-17.711172380623,17.0294022813644));
#179183=CARTESIAN_POINT('Ctrl Pts',(20.4053569830019,-17.6524781588698,
17.0252478948409));
#179184=CARTESIAN_POINT('Ctrl Pts',(20.3915070883327,-17.6348585946878,
17.0239968303872));
#179185=CARTESIAN_POINT('Ctrl Pts',(20.3484520641552,-17.5818396882788,
17.0202092363147));
#179186=CARTESIAN_POINT('Ctrl Pts',(20.3183729706973,-17.5471664592261,
17.0176999688148));
#179187=CARTESIAN_POINT('Ctrl Pts',(20.2128851959383,-17.4332684728602,
17.0092478755073));
#179188=CARTESIAN_POINT('Ctrl Pts',(20.1324765156178,-17.3589182613142,
17.0033596732591));
#179189=CARTESIAN_POINT('Ctrl Pts',(20.0034493180968,-17.2569410477388,
16.994215076586));
#179190=CARTESIAN_POINT('Ctrl Pts',(19.9588953967741,-17.2244708267689,
16.9911074109248));
#179191=CARTESIAN_POINT('Ctrl Pts',(19.8846332442519,-17.1746679440795,
16.9859631747503));
#179192=CARTESIAN_POINT('Ctrl Pts',(19.855679797452,-17.1562549359242,16.9839659964122));
#179193=CARTESIAN_POINT('Ctrl Pts',(19.8170337188935,-17.1329772405272,
16.9813052732521));
#179194=CARTESIAN_POINT('Ctrl Pts',(19.8077321153054,-17.1274712461177,
16.9806652584713));
#179195=CARTESIAN_POINT('Ctrl Pts',(19.7924259804511,-17.118568509827,16.9796125412864));
#179196=CARTESIAN_POINT('Ctrl Pts',(19.786446216972,-17.1151294155816,16.9792013802263));
#179197=CARTESIAN_POINT('Ctrl Pts',(19.7748369760338,-17.1085279823513,
16.9784033106653));
#179198=CARTESIAN_POINT('Ctrl Pts',(19.769209622997,-17.1053620480574,16.9780165375546));
#179199=CARTESIAN_POINT('Ctrl Pts',(19.7561804757564,-17.0981101553555,
16.9771211633197));
#179200=CARTESIAN_POINT('Ctrl Pts',(19.7487685488852,-17.0940427157634,
16.9766119060867));
#179201=CARTESIAN_POINT('Ctrl Pts',(19.7287642138754,-17.0832203569117,
16.9752376125887));
#179202=CARTESIAN_POINT('Ctrl Pts',(19.7161276161237,-17.0765484475575,
16.9743696483561));
#179203=CARTESIAN_POINT('Ctrl Pts',(19.5995634299499,-17.0165056710283,
16.9663634959402));
#179204=CARTESIAN_POINT('Ctrl Pts',(19.4914690089998,-16.9717042529663,
16.9589236278741));
#179205=CARTESIAN_POINT('Ctrl Pts',(19.2253472622209,-16.8863943993965,
16.940669498441));
#179206=CARTESIAN_POINT('Ctrl Pts',(19.0652449898105,-16.8547576559061,
16.9297153297797));
#179207=CARTESIAN_POINT('Ctrl Pts',(18.870625616796,-16.8391621396681,16.9173083171974));
#179208=CARTESIAN_POINT('Ctrl Pts',(18.8380929695566,-16.8373096427298,
16.9152663165047));
#179209=CARTESIAN_POINT('Ctrl Pts',(18.7982882165433,-16.8359639635512,
16.9128171881611));
#179210=CARTESIAN_POINT('Ctrl Pts',(18.7910465536276,-16.8357563522717,
16.9123736142436));
#179211=CARTESIAN_POINT('Ctrl Pts',(18.7796942477205,-16.8354892077068,
16.911681528221));
#179212=CARTESIAN_POINT('Ctrl Pts',(18.7755843338242,-16.8354044689614,
16.9114316430668));
#179213=CARTESIAN_POINT('Ctrl Pts',(18.7679029855719,-16.8352684759644,
16.9109659035768));
#179214=CARTESIAN_POINT('Ctrl Pts',(18.7643317075639,-16.8352142892998,
16.9107498933849));
#179215=CARTESIAN_POINT('Ctrl Pts',(18.7561808611843,-16.8351112491809,
16.9102580684049));
#179216=CARTESIAN_POINT('Ctrl Pts',(18.75160126969,-16.8350682178783,16.9099825822549));
#179217=CARTESIAN_POINT('Ctrl Pts',(18.7375304072785,-16.8349816673078,
16.9091386543664));
#179218=CARTESIAN_POINT('Ctrl Pts',(18.7280388039128,-16.8349871147156,
16.9085728815195));
#179219=CARTESIAN_POINT('Ctrl Pts',(18.6430927357192,-16.8356071789726,
16.9035382645834));
#179220=CARTESIAN_POINT('Ctrl Pts',(18.5677126421295,-16.8401918211874,
16.8992734412857));
#179221=CARTESIAN_POINT('Ctrl Pts',(18.4499500110904,-16.8537009554024,
16.8927111952766));
#179222=CARTESIAN_POINT('Ctrl Pts',(18.4073278166062,-16.8599128238263,
16.8903571658276));
#179223=CARTESIAN_POINT('Ctrl Pts',(18.2572736260032,-16.8864800209564,
16.8820606563415));
#179224=CARTESIAN_POINT('Ctrl Pts',(18.1512626662309,-16.9138495804539,
16.8761738091633));
#179225=CARTESIAN_POINT('Ctrl Pts',(17.995737716435,-16.9671343761917,16.8670323627783));
#179226=CARTESIAN_POINT('Ctrl Pts',(17.9443513733083,-16.9870121766752,
16.8639265027801));
#179227=CARTESIAN_POINT('Ctrl Pts',(17.8623237772519,-17.0224804674919,
16.8587849891377));
#179228=CARTESIAN_POINT('Ctrl Pts',(17.8311833444689,-17.0368532813996,
16.8567886730124));
#179229=CARTESIAN_POINT('Ctrl Pts',(17.7907073085509,-17.0567415225125,
16.8541289357708));
#179230=CARTESIAN_POINT('Ctrl Pts',(17.781044427072,-17.0615816685984,16.8534890224442));
#179231=CARTESIAN_POINT('Ctrl Pts',(17.765275619888,-17.0696319022643,16.8524364296291));
#179232=CARTESIAN_POINT('Ctrl Pts',(17.7591474991179,-17.0727982599548,
16.8520252907696));
#179233=CARTESIAN_POINT('Ctrl Pts',(17.747313090532,-17.0789864829095,16.8512272339164));
#179234=CARTESIAN_POINT('Ctrl Pts',(17.7416049319149,-17.0820046203462,
16.8508404511521));
#179235=CARTESIAN_POINT('Ctrl Pts',(17.7284538608288,-17.0890353038905,
16.8499450102998));
#179236=CARTESIAN_POINT('Ctrl Pts',(17.7210210398499,-17.0930664024755,
16.8494356957957));
#179237=CARTESIAN_POINT('Ctrl Pts',(17.7010895643663,-17.1040310283788,
16.84806114753));
#179238=CARTESIAN_POINT('Ctrl Pts',(17.6886368158597,-17.1110466910775,
16.8471929841115));
#179239=CARTESIAN_POINT('Ctrl Pts',(17.5748400110784,-17.1766847385948,
16.839171510024));
#179240=CARTESIAN_POINT('Ctrl Pts',(17.4784677450456,-17.2434839586772,
16.8317151784735));
#179241=CARTESIAN_POINT('Ctrl Pts',(17.2619561354151,-17.4218067422182,
16.8133920003601));
#179242=CARTESIAN_POINT('Ctrl Pts',(17.1482518540488,-17.5399774970377,
16.8023832044535));
#179243=CARTESIAN_POINT('Ctrl Pts',(17.0301039703484,-17.6952463971379,
16.7899955315845));
#179244=CARTESIAN_POINT('Ctrl Pts',(17.0114991784074,-17.7208694354002,
16.7880124611225));
#179245=CARTESIAN_POINT('Ctrl Pts',(16.9893874427833,-17.7528054419641,
16.7856241526983));
#179246=CARTESIAN_POINT('Ctrl Pts',(16.9853298243766,-17.7587300460031,
16.7851845272729));
#179247=CARTESIAN_POINT('Ctrl Pts',(16.9790047132035,-17.7680670093458,
16.7844972263259));
#179248=CARTESIAN_POINT('Ctrl Pts',(16.9767168904267,-17.7714654361251,
16.784248208229));
#179249=CARTESIAN_POINT('Ctrl Pts',(16.9724517498487,-17.7778409244991,
16.7837832155224));
#179250=CARTESIAN_POINT('Ctrl Pts',(16.9704721279198,-17.780816318075,16.783567090291));
#179251=CARTESIAN_POINT('Ctrl Pts',(16.9659610004637,-17.7876339636287,
16.7830738731386));
#179252=CARTESIAN_POINT('Ctrl Pts',(16.9634344849883,-17.7914794579568,
16.7827971170523));
#179253=CARTESIAN_POINT('Ctrl Pts',(16.9568582374412,-17.8015603297506,
16.7820752899555));
#179254=CARTESIAN_POINT('Ctrl Pts',(16.9528287407576,-17.8078089197858,
16.7816315358764));
#179255=CARTESIAN_POINT('Ctrl Pts',(16.9262822845475,-17.8494549280485,
16.7786973474529));
#179256=CARTESIAN_POINT('Ctrl Pts',(16.9047872114559,-17.8854963304429,
16.7762696353254));
#179257=CARTESIAN_POINT('Ctrl Pts',(16.8738142378991,-17.941124484184,16.7726519437717));
#179258=CARTESIAN_POINT('Ctrl Pts',(16.8635446403685,-17.9602554880022,
16.7714302374583));
#179259=CARTESIAN_POINT('Ctrl Pts',(16.8457278215645,-17.9947076192241,
16.7692640336148));
#179260=CARTESIAN_POINT('Ctrl Pts',(16.8380683858714,-18.0099682299352,
16.768316156312));
#179261=CARTESIAN_POINT('Ctrl Pts',(16.7987610397288,-18.0907057371168,
16.7633540382376));
#179262=CARTESIAN_POINT('Ctrl Pts',(16.7703355293929,-18.1576524547246,
16.7594186555602));
#179263=CARTESIAN_POINT('Ctrl Pts',(16.7454192974512,-18.2258899605083,
16.7554728927777));
#179264=CARTESIAN_POINT('',(16.6170000778107,-18.9514260221329,17.2909082085163));
#179265=CARTESIAN_POINT('Ctrl Pts',(16.7454193692319,-18.2258897639242,
16.5356516076535));
#179266=CARTESIAN_POINT('Ctrl Pts',(16.7457579316466,-18.2249625511863,
16.5357110070265));
#179267=CARTESIAN_POINT('Ctrl Pts',(16.7460971434404,-18.2240355728191,
16.5357703682188));
#179268=CARTESIAN_POINT('Ctrl Pts',(16.7488929534975,-18.2164118714529,
16.5362583814801));
#179269=CARTESIAN_POINT('Ctrl Pts',(16.7513827741478,-18.2097272603787,
16.5366850874225));
#179270=CARTESIAN_POINT('Ctrl Pts',(16.7648702365569,-18.1740685038746,
16.5389555844351));
#179271=CARTESIAN_POINT('Ctrl Pts',(16.7764699452589,-18.1453242589646,
16.5407654901067));
#179272=CARTESIAN_POINT('Ctrl Pts',(16.8532263795245,-17.9665380260565,
16.5519560730976));
#179273=CARTESIAN_POINT('Ctrl Pts',(16.9349647273724,-17.8242016348003,
16.5606012080705));
#179274=CARTESIAN_POINT('Ctrl Pts',(17.1022875653794,-17.598098072237,16.5759957187365));
#179275=CARTESIAN_POINT('Ctrl Pts',(17.1800410103599,-17.5095222650219,
16.58256213577));
#179276=CARTESIAN_POINT('Ctrl Pts',(17.2750386749844,-17.4179447995518,
16.590292142767));
#179277=CARTESIAN_POINT('Ctrl Pts',(17.2854344416404,-17.4081245794737,
16.591134269601));
#179278=CARTESIAN_POINT('Ctrl Pts',(17.3021355858462,-17.3926652592262,
16.5924816547495));
#179279=CARTESIAN_POINT('Ctrl Pts',(17.3083767594504,-17.3869572187501,
16.5929839662928));
#179280=CARTESIAN_POINT('Ctrl Pts',(17.3194429380778,-17.3769574558901,
16.5938725894741));
#179281=CARTESIAN_POINT('Ctrl Pts',(17.3242537156038,-17.3726500991246,
16.5942582340704));
#179282=CARTESIAN_POINT('Ctrl Pts',(17.3342433738404,-17.3637878116787,
16.5950577033534));
#179283=CARTESIAN_POINT('Ctrl Pts',(17.3394249519492,-17.359236049751,16.5954716538736));
#179284=CARTESIAN_POINT('Ctrl Pts',(17.3527797460429,-17.3476196460923,
16.5965367450822));
#179285=CARTESIAN_POINT('Ctrl Pts',(17.3609848905063,-17.3405921645117,
16.5971894129516));
#179286=CARTESIAN_POINT('Ctrl Pts',(17.3954326586002,-17.3115427138292,
16.5999226832476));
#179287=CARTESIAN_POINT('Ctrl Pts',(17.4221529057372,-17.2900975897885,
16.6020265575377));
#179288=CARTESIAN_POINT('Ctrl Pts',(17.4930983435437,-17.2359355321594,
16.6075743393707));
#179289=CARTESIAN_POINT('Ctrl Pts',(17.538096974659,-17.2042788219609,16.6110565170793));
#179290=CARTESIAN_POINT('Ctrl Pts',(17.6611866045542,-17.1246657032057,
16.6204782806145));
#179291=CARTESIAN_POINT('Ctrl Pts',(17.7412413669288,-17.0799670751409,
16.6265050358633));
#179292=CARTESIAN_POINT('Ctrl Pts',(17.8723898346,-17.017524021557,16.6361026784844));
#179293=CARTESIAN_POINT('Ctrl Pts',(17.9217074221706,-16.996303110698,16.639652561429));
#179294=CARTESIAN_POINT('Ctrl Pts',(18.0061489782579,-16.9637145194573,
16.645587331596));
#179295=CARTESIAN_POINT('Ctrl Pts',(18.0408609965526,-16.9513489079362,
16.6479873598333));
#179296=CARTESIAN_POINT('Ctrl Pts',(18.1208694487278,-16.9251796859873,
16.6534054177813));
#179297=CARTESIAN_POINT('Ctrl Pts',(18.166344442657,-16.9119760836724,16.6564034619504));
#179298=CARTESIAN_POINT('Ctrl Pts',(18.2196941097344,-16.8984085587801,
16.6597974543887));
#179299=CARTESIAN_POINT('Ctrl Pts',(18.2271711786098,-16.8965504369703,
16.6602703428091));
#179300=CARTESIAN_POINT('Ctrl Pts',(18.2391594155229,-16.8936406414161,
16.6610238999646));
#179301=CARTESIAN_POINT('Ctrl Pts',(18.2436640998979,-16.8925629023622,
16.6613060095215));
#179302=CARTESIAN_POINT('Ctrl Pts',(18.2516628015271,-16.890676956991,16.6618050353246));
#179303=CARTESIAN_POINT('Ctrl Pts',(18.2551553772695,-16.8898628346593,
16.662022288459));
#179304=CARTESIAN_POINT('Ctrl Pts',(18.262578318197,-16.8881524164112,16.6624826492754));
#179305=CARTESIAN_POINT('Ctrl Pts',(18.2665091707841,-16.8872584724516,
16.6627256213737));
#179306=CARTESIAN_POINT('Ctrl Pts',(18.2771600196659,-16.8848682604252,
16.6633818228253));
#179307=CARTESIAN_POINT('Ctrl Pts',(18.2838848677486,-16.8833935204877,
16.6637938345701));
#179308=CARTESIAN_POINT('Ctrl Pts',(18.3177490238762,-16.8761401661215,
16.6658575410414));
#179309=CARTESIAN_POINT('Ctrl Pts',(18.3449942703993,-16.8708624181691,
16.667482244176));
#179310=CARTESIAN_POINT('Ctrl Pts',(18.4247162617235,-16.8570397014274,
16.6721533891327));
#179311=CARTESIAN_POINT('Ctrl Pts',(18.4774228910061,-16.8499333875376,
16.6751378899842));
#179312=CARTESIAN_POINT('Ctrl Pts',(18.6704674242955,-16.8312759601424,
16.6858683621127));
#179313=CARTESIAN_POINT('Ctrl Pts',(18.8115927598804,-16.8317433080845,
16.6933518959393));
#179314=CARTESIAN_POINT('Ctrl Pts',(19.0430308398618,-16.8556622025063,
16.7062219698052));
#179315=CARTESIAN_POINT('Ctrl Pts',(19.1337087864596,-16.8710477869865,
16.7114143335807));
#179316=CARTESIAN_POINT('Ctrl Pts',(19.2364858658513,-16.8954527946891,
16.7176070908601));
#179317=CARTESIAN_POINT('Ctrl Pts',(19.2498461121305,-16.8987632313086,
16.7184180563041));
#179318=CARTESIAN_POINT('Ctrl Pts',(19.2712106903153,-16.9042786844685,
16.7197248421897));
#179319=CARTESIAN_POINT('Ctrl Pts',(19.2792361207256,-16.906400948003,16.720217990276));
#179320=CARTESIAN_POINT('Ctrl Pts',(19.2934578943537,-16.9102514249627,
16.721096000627));
#179321=CARTESIAN_POINT('Ctrl Pts',(19.2996592653873,-16.9119607912364,
16.7214802470044));
#179322=CARTESIAN_POINT('Ctrl Pts',(19.3125582726307,-16.9155796531408,
16.7222824324488));
#179323=CARTESIAN_POINT('Ctrl Pts',(19.3192544605672,-16.9174939866115,
16.7227005251823));
#179324=CARTESIAN_POINT('Ctrl Pts',(19.3366078024684,-16.9225477914207,
16.7237883917691));
#179325=CARTESIAN_POINT('Ctrl Pts',(19.3472498035017,-16.9257381458365,
16.7244598207519));
#179326=CARTESIAN_POINT('Ctrl Pts',(19.3932464610423,-16.9399229822027,
16.7273808223348));
#179327=CARTESIAN_POINT('Ctrl Pts',(19.4283326608282,-16.9517595878086,
16.7296578511468));
#179328=CARTESIAN_POINT('Ctrl Pts',(19.520606171892,-16.9856091004283,16.7357809459443));
#179329=CARTESIAN_POINT('Ctrl Pts',(19.577175806304,-17.0091938088539,16.7396759213215));
#179330=CARTESIAN_POINT('Ctrl Pts',(19.7735717689237,-17.1012685187257,
16.7536844023944));
#179331=CARTESIAN_POINT('Ctrl Pts',(19.9067736508129,-17.1826745555084,
16.7641302935602));
#179332=CARTESIAN_POINT('Ctrl Pts',(20.0425288699526,-17.287758870077,16.7752910035534));
#179333=CARTESIAN_POINT('Ctrl Pts',(20.0551025450465,-17.2977223849462,
16.7763295833007));
#179334=CARTESIAN_POINT('Ctrl Pts',(20.1049633123591,-17.338163668473,16.780464122607));
#179335=CARTESIAN_POINT('Ctrl Pts',(20.141321947888,-17.3697693492074,16.7835157651995));
#179336=CARTESIAN_POINT('Ctrl Pts',(20.1822398024961,-17.4078658054716,
16.786963012381));
#179337=CARTESIAN_POINT('Ctrl Pts',(20.1878770983402,-17.413172419222,16.7874382343839));
#179338=CARTESIAN_POINT('Ctrl Pts',(20.1968483347533,-17.4217107120478,
16.7881947875875));
#179339=CARTESIAN_POINT('Ctrl Pts',(20.2002009138202,-17.4249225833077,
16.7884775774023));
#179340=CARTESIAN_POINT('Ctrl Pts',(20.2061253709757,-17.4306358873811,
16.7889773728589));
#179341=CARTESIAN_POINT('Ctrl Pts',(20.2087014888055,-17.4331328594372,
16.7891947190711));
#179342=CARTESIAN_POINT('Ctrl Pts',(20.2141542441453,-17.4384450412243,
16.7896547982651));
#179343=CARTESIAN_POINT('Ctrl Pts',(20.2170291983152,-17.4412619031539,
16.7898973981151));
#179344=CARTESIAN_POINT('Ctrl Pts',(20.2247797112398,-17.4488992515652,
16.7905515404179));
#179345=CARTESIAN_POINT('Ctrl Pts',(20.2296399630892,-17.453735300043,16.7909618782856));
#179346=CARTESIAN_POINT('Ctrl Pts',(20.2538070883146,-17.4780168628845,
16.7930034478209));
#179347=CARTESIAN_POINT('Ctrl Pts',(20.2727595998508,-17.497813310003,16.794608376622));
#179348=CARTESIAN_POINT('Ctrl Pts',(20.3266669183098,-17.5563555408519,
16.7992046181021));
#179349=CARTESIAN_POINT('Ctrl Pts',(20.360581867575,-17.5960340951197,16.8021363322757));
#179350=CARTESIAN_POINT('Ctrl Pts',(20.4796153933748,-17.7461980123186,
16.8127466170172));
#179351=CARTESIAN_POINT('Ctrl Pts',(20.5552265603972,-17.8637593465706,
16.8201606503024));
#179352=CARTESIAN_POINT('Ctrl Pts',(20.6617591792953,-18.0720223132515,
16.8330840696799));
#179353=CARTESIAN_POINT('Ctrl Pts',(20.6991033001663,-18.1589161504293,
16.8384165267062));
#179354=CARTESIAN_POINT('Ctrl Pts',(20.7351175527663,-18.2610521829524,
16.8447649157734));
#179355=CARTESIAN_POINT('Ctrl Pts',(20.7395894900493,-18.2741422496332,
16.8455798672138));
#179356=CARTESIAN_POINT('Ctrl Pts',(20.746545628087,-18.2951755627874,16.846891852208));
#179357=CARTESIAN_POINT('Ctrl Pts',(20.7491118760681,-18.3030914006092,
16.8473861790022));
#179358=CARTESIAN_POINT('Ctrl Pts',(20.7535799444679,-18.3171557148462,
16.848265547018));
#179359=CARTESIAN_POINT('Ctrl Pts',(20.7555005328611,-18.3232981527626,
16.8486499657966));
#179360=CARTESIAN_POINT('Ctrl Pts',(20.7594384278194,-18.3360969627027,
16.8494517650095));
#179361=CARTESIAN_POINT('Ctrl Pts',(20.7614509958386,-18.3427547013591,
16.8498692954058));
#179362=CARTESIAN_POINT('Ctrl Pts',(20.7665811782359,-18.3600327179641,
16.8509540754894));
#179363=CARTESIAN_POINT('Ctrl Pts',(20.7696483469128,-18.3706676427868,
16.8516229627504));
#179364=CARTESIAN_POINT('Ctrl Pts',(20.7825082896349,-18.4166075116827,
16.854517792768));
#179365=CARTESIAN_POINT('Ctrl Pts',(20.7914665648738,-18.4521376183938,
16.8567705860487));
#179366=CARTESIAN_POINT('Ctrl Pts',(20.8127333699572,-18.5467825422329,
16.8628119273177));
#179367=CARTESIAN_POINT('Ctrl Pts',(20.8234420278755,-18.6062189063305,
16.8666477812295));
#179368=CARTESIAN_POINT('Ctrl Pts',(20.8539096070944,-18.8296972741524,
16.8812045005653));
#179369=CARTESIAN_POINT('Ctrl Pts',(20.8569895064341,-18.9953986078187,
16.8923178090366));
#179370=CARTESIAN_POINT('Ctrl Pts',(20.8402747663553,-19.1648899587749,
16.9033404905975));
#179371=CARTESIAN_POINT('Ctrl Pts',(20.8397506016606,-19.1700136010275,
16.9036733163694));
#179372=CARTESIAN_POINT('Ctrl Pts',(20.8385402686491,-19.1814326919621,
16.9044141620626));
#179373=CARTESIAN_POINT('Ctrl Pts',(20.8378445375761,-19.1877270998669,
16.9048219020755));
#179374=CARTESIAN_POINT('Ctrl Pts',(20.8319910254868,-19.2385936639612,
16.9081114066809));
#179375=CARTESIAN_POINT('Ctrl Pts',(20.8254451925663,-19.2829983820863,
16.9109488191941));
#179376=CARTESIAN_POINT('Ctrl Pts',(20.8161485353515,-19.3346277269972,
16.9141824039571));
#179377=CARTESIAN_POINT('Ctrl Pts',(20.8147646143112,-19.3420834840355,
16.9146477509915));
#179378=CARTESIAN_POINT('Ctrl Pts',(20.8124775967123,-19.3540460213231,
16.9153916170681));
#179379=CARTESIAN_POINT('Ctrl Pts',(20.8115998471143,-19.3585574983769,
16.9156715200884));
#179380=CARTESIAN_POINT('Ctrl Pts',(20.8100119342341,-19.3665796393241,
16.9161680605031));
#179381=CARTESIAN_POINT('Ctrl Pts',(20.8093075464648,-19.3700913975676,
16.9163850228345));
#179382=CARTESIAN_POINT('Ctrl Pts',(20.8077872269704,-19.3775725061254,
16.9168463485946));
#179383=CARTESIAN_POINT('Ctrl Pts',(20.8069688120972,-19.3815412965269,
16.9170905682988));
#179384=CARTESIAN_POINT('Ctrl Pts',(20.8047097734705,-19.3923393549919,
16.9177536780116));
#179385=CARTESIAN_POINT('Ctrl Pts',(20.8032467497388,-19.3991639579512,
16.9181713062858));
#179386=CARTESIAN_POINT('Ctrl Pts',(20.7955436669008,-19.4342492116117,
16.9203113336856));
#179387=CARTESIAN_POINT('Ctrl Pts',(20.7887579865491,-19.4623884771996,
16.9220042938675));
#179388=CARTESIAN_POINT('Ctrl Pts',(20.7669925003292,-19.545159912836,16.9269383504506));
#179389=CARTESIAN_POINT('Ctrl Pts',(20.7503942898981,-19.5993423806615,
16.9301088958517));
#179390=CARTESIAN_POINT('Ctrl Pts',(20.6842689006648,-19.7878345898215,
16.9411316553532));
#179391=CARTESIAN_POINT('Ctrl Pts',(20.6233265152133,-19.9177200611084,
16.9487391883837));
#179392=CARTESIAN_POINT('Ctrl Pts',(20.5287380642251,-20.0755094955522,
16.9589508547083));
#179393=CARTESIAN_POINT('Ctrl Pts',(20.506721953469,-20.1099356347493,16.9612417048194));
#179394=CARTESIAN_POINT('Ctrl Pts',(20.4565623206211,-20.1835828464794,
16.9663073414754));
#179395=CARTESIAN_POINT('Ctrl Pts',(20.4280464712532,-20.2225208723823,
16.9690932490908));
#179396=CARTESIAN_POINT('Ctrl Pts',(20.3904563072864,-20.2703321145388,
16.972670343423));
#179397=CARTESIAN_POINT('Ctrl Pts',(20.3825980338955,-20.2801459161364,
16.9734131972958));
#179398=CARTESIAN_POINT('Ctrl Pts',(20.370000609189,-20.2955941350155,16.9745965841451));
#179399=CARTESIAN_POINT('Ctrl Pts',(20.3653185987138,-20.3012749239152,
16.9750348091776));
#179400=CARTESIAN_POINT('Ctrl Pts',(20.3565353225848,-20.3118193265516,
16.9758540025463));
#179401=CARTESIAN_POINT('Ctrl Pts',(20.3524415674669,-20.3166891093673,
16.9762346616875));
#179402=CARTESIAN_POINT('Ctrl Pts',(20.3432950899046,-20.3274703882299,
16.9770826379979));
#179403=CARTESIAN_POINT('Ctrl Pts',(20.3382316379539,-20.3333726233566,
16.9775503943819));
#179404=CARTESIAN_POINT('Ctrl Pts',(20.3234078905989,-20.3504605605342,
16.9789150281003));
#179405=CARTESIAN_POINT('Ctrl Pts',(20.313562464884,-20.3615714894902,16.9798154384965));
#179406=CARTESIAN_POINT('Ctrl Pts',(20.2335265870203,-20.4500034041803,
16.9870893252779));
#179407=CARTESIAN_POINT('Ctrl Pts',(20.1578298999202,-20.5221264019524,
16.9937011742737));
#179408=CARTESIAN_POINT('Ctrl Pts',(19.947192608373,-20.69501811552,17.0114031389657));
#179409=CARTESIAN_POINT('Ctrl Pts',(19.8050215000256,-20.7858096987755,
17.0227380649217));
#179410=CARTESIAN_POINT('Ctrl Pts',(19.6178491272122,-20.8760780578777,
17.0360339347626));
#179411=CARTESIAN_POINT('Ctrl Pts',(19.5816031288803,-20.8923182868501,
17.0385365138317));
#179412=CARTESIAN_POINT('Ctrl Pts',(19.5381637633804,-20.9103317198838,
17.0414334940262));
#179413=CARTESIAN_POINT('Ctrl Pts',(19.5313937441473,-20.9130980862233,
17.041882090998));
#179414=CARTESIAN_POINT('Ctrl Pts',(19.5203752769399,-20.9175339624139,
17.0426073443738));
#179415=CARTESIAN_POINT('Ctrl Pts',(19.5161355923517,-20.9192248853812,
17.0428852452359));
#179416=CARTESIAN_POINT('Ctrl Pts',(19.508569916496,-20.9222139963249,17.043379045138));
#179417=CARTESIAN_POINT('Ctrl Pts',(19.5052460858614,-20.923517492325,17.0435952602193));
#179418=CARTESIAN_POINT('Ctrl Pts',(19.4980785171377,-20.9263074742307,
17.0440599397931));
#179419=CARTESIAN_POINT('Ctrl Pts',(19.4942337430918,-20.9277911427286,
17.0443082346788));
#179420=CARTESIAN_POINT('Ctrl Pts',(19.4835744358103,-20.9318687660506,
17.0449940057983));
#179421=CARTESIAN_POINT('Ctrl Pts',(19.4767507216162,-20.9344387845927,
17.0454300708023));
#179422=CARTESIAN_POINT('Ctrl Pts',(19.438712247109,-20.9485412579937,17.047845277202));
#179423=CARTESIAN_POINT('Ctrl Pts',(19.4072403424395,-20.9593724284508,
17.0497852111968));
#179424=CARTESIAN_POINT('Ctrl Pts',(19.2210809313221,-21.0185685993613,
17.0609920754098));
#179425=CARTESIAN_POINT('Ctrl Pts',(19.0614935560465,-21.0497876801291,
17.0695592837018));
#179426=CARTESIAN_POINT('Ctrl Pts',(18.7836239819198,-21.0716293086547,
17.0848192198537));
#179427=CARTESIAN_POINT('Ctrl Pts',(18.6668143820672,-21.0711441191033,
17.0913306623629));
#179428=CARTESIAN_POINT('Ctrl Pts',(18.5364141023222,-21.0598076140108,
17.0989987893772));
#179429=CARTESIAN_POINT('Ctrl Pts',(18.5221937291252,-21.0584261708781,
17.0998401416315));
#179430=CARTESIAN_POINT('Ctrl Pts',(18.4995830679418,-21.0559983771151,
17.1011865188859));
#179431=CARTESIAN_POINT('Ctrl Pts',(18.4911830299834,-21.0550455023247,
17.1016886040876));
#179432=CARTESIAN_POINT('Ctrl Pts',(18.4763779343099,-21.0532761742023,
17.1025769635994));
#179433=CARTESIAN_POINT('Ctrl Pts',(18.469970446441,-21.0524806788977,17.1029625721368));
#179434=CARTESIAN_POINT('Ctrl Pts',(18.4567247734735,-21.0507746515551,
17.1037621009545));
#179435=CARTESIAN_POINT('Ctrl Pts',(18.4498872070014,-21.0498599830203,
17.1041761477307));
#179436=CARTESIAN_POINT('Ctrl Pts',(18.4323464890353,-21.0474262152985,
17.1052417694463));
#179437=CARTESIAN_POINT('Ctrl Pts',(18.4216503789837,-21.045858536745,17.1058948745054));
#179438=CARTESIAN_POINT('Ctrl Pts',(18.377048252512,-21.0389720530882,17.1086323803955));
#179439=CARTESIAN_POINT('Ctrl Pts',(18.3432636531629,-21.0329112886132,
17.1107401434045));
#179440=CARTESIAN_POINT('Ctrl Pts',(18.2556228290471,-21.0149795443641,
17.1163006257816));
#179441=CARTESIAN_POINT('Ctrl Pts',(18.2020593553583,-21.0018213693875,
17.1197918341491));
#179442=CARTESIAN_POINT('Ctrl Pts',(18.0413674195267,-20.9556238690923,
17.1305393375562));
#179443=CARTESIAN_POINT('Ctrl Pts',(17.9362970231054,-20.9161575271391,
17.1379542076809));
#179444=CARTESIAN_POINT('Ctrl Pts',(17.7301970838325,-20.8194668160528,
17.1529889026018));
#179445=CARTESIAN_POINT('Ctrl Pts',(17.6297255448464,-20.7618720390721,
17.1605809871905));
#179446=CARTESIAN_POINT('Ctrl Pts',(17.5265614332745,-20.6909286316569,
17.1683149651159));
#179447=CARTESIAN_POINT('Ctrl Pts',(17.5187086993475,-20.6854496649405,
17.1689031869773));
#179448=CARTESIAN_POINT('Ctrl Pts',(17.5071418491718,-20.6772620676196,
17.1697685805832));
#179449=CARTESIAN_POINT('Ctrl Pts',(17.5033990733629,-20.6745944051054,
17.1700484399808));
#179450=CARTESIAN_POINT('Ctrl Pts',(17.4968473584393,-20.6698924207961,
17.1705380032819));
#179451=CARTESIAN_POINT('Ctrl Pts',(17.4940347034429,-20.6678633663296,
17.1707480641273));
#179452=CARTESIAN_POINT('Ctrl Pts',(17.4912141761505,-20.6658180756104,
17.170958598793));
#179453=CARTESIAN_POINT('Ctrl Pts',(17.4912013661276,-20.6658087862697,
17.1709595549785));
#179454=CARTESIAN_POINT('Ctrl Pts',(17.4911759712835,-20.6657903704615,
17.1709614505352));
#179455=CARTESIAN_POINT('Ctrl Pts',(17.4911633862972,-20.6657812438819,
17.1709623899187));
#179456=CARTESIAN_POINT('Ctrl Pts',(17.4911384362608,-20.6657631498002,
17.1709642522647));
#179457=CARTESIAN_POINT('Ctrl Pts',(17.4911260712267,-20.665754182317,17.170965175226));
#179458=CARTESIAN_POINT('Ctrl Pts',(17.4911015560354,-20.6657364027807,
17.1709670051054));
#179459=CARTESIAN_POINT('Ctrl Pts',(17.4910894058864,-20.6657275907405,
17.1709679120229));
#179460=CARTESIAN_POINT('Ctrl Pts',(17.491065316964,-20.6657101195721,17.1709697100762));
#179461=CARTESIAN_POINT('Ctrl Pts',(17.4910533776243,-20.6657014600397,
17.1709706012544));
#179462=CARTESIAN_POINT('Ctrl Pts',(17.4910297034798,-20.6656842889455,
17.1709723683399));
#179463=CARTESIAN_POINT('Ctrl Pts',(17.4910179695274,-20.6656757780083,
17.1709732441836));
#179464=CARTESIAN_POINT('Ctrl Pts',(17.4909947029493,-20.6656589017967,
17.1709749808399));
#179465=CARTESIAN_POINT('Ctrl Pts',(17.4909831701517,-20.6656505364037,
17.1709758416654));
#179466=CARTESIAN_POINT('Ctrl Pts',(17.4909603023359,-20.6656339487263,
17.17097754855));
#179467=CARTESIAN_POINT('Ctrl Pts',(17.4909489668599,-20.6656257261157,
17.1709783946435));
#179468=CARTESIAN_POINT('Ctrl Pts',(17.4909264872925,-20.665609419382,17.1709800725417));
#179469=CARTESIAN_POINT('Ctrl Pts',(17.4909153440214,-20.6656013358597,
17.1709809042852));
#179470=CARTESIAN_POINT('Ctrl Pts',(17.4908932467853,-20.6655853058121,
17.170982553639));
#179471=CARTESIAN_POINT('Ctrl Pts',(17.4908822922737,-20.6655773588959,
17.17098337129));
#179472=CARTESIAN_POINT('Ctrl Pts',(17.4908605676019,-20.6655615984825,
17.1709849928286));
#179473=CARTESIAN_POINT('Ctrl Pts',(17.4908497975491,-20.6655537850687,
17.1709857967083));
#179474=CARTESIAN_POINT('Ctrl Pts',(17.4908284382772,-20.6655382891242,
17.1709873909669));
#179475=CARTESIAN_POINT('Ctrl Pts',(17.4908178489378,-20.6655306065115,
17.1709881813549));
#179476=CARTESIAN_POINT('Ctrl Pts',(17.4907968468906,-20.6655153691357,
17.1709897489441));
#179477=CARTESIAN_POINT('Ctrl Pts',(17.4907864342944,-20.6655078144587,
17.170990526137));
#179478=CARTESIAN_POINT('Ctrl Pts',(17.4907663390662,-20.6654932344378,
17.1709920260355));
#179479=CARTESIAN_POINT('Ctrl Pts',(17.4907566562433,-20.6654862089751,
17.1709927487556));
#179480=CARTESIAN_POINT('Ctrl Pts',(17.4907373266925,-20.6654721839885,
17.1709941914991));
#179481=CARTESIAN_POINT('Ctrl Pts',(17.4907276802347,-20.6654651846616,
17.1709949115024));
#179482=CARTESIAN_POINT('Ctrl Pts',(17.4907084234582,-20.6654512119816,
17.170996348809));
#179483=CARTESIAN_POINT('Ctrl Pts',(17.4906988130375,-20.6654442385553,
17.1709970661199));
#179484=CARTESIAN_POINT('Ctrl Pts',(17.4906796287385,-20.6654303179722,
17.1709984980117));
#179485=CARTESIAN_POINT('Ctrl Pts',(17.4906700543764,-20.6654233704649,
17.1709992126287));
#179486=CARTESIAN_POINT('Ctrl Pts',(17.4906509412146,-20.6654095010115,
17.1710006392058));
#179487=CARTESIAN_POINT('Ctrl Pts',(17.4906414025766,-20.6654025791834,
17.1710013511538));
#179488=CARTESIAN_POINT('Ctrl Pts',(17.4873373597135,-20.6630049183732,
17.1712479589786));
#179489=CARTESIAN_POINT('Ctrl Pts',(17.4840497265218,-20.6606046599071,
17.171493191571));
#179490=CARTESIAN_POINT('Ctrl Pts',(17.4772529883802,-20.6556123329168,
17.1719999110107));
#179491=CARTESIAN_POINT('Ctrl Pts',(17.4737449279074,-20.6530188670642,
17.1722613008812));
#179492=CARTESIAN_POINT('Ctrl Pts',(17.4648423050744,-20.6463946096127,
17.1729243398703));
#179493=CARTESIAN_POINT('Ctrl Pts',(17.4594588676324,-20.6423488551926,
17.1733249935635));
#179494=CARTESIAN_POINT('Ctrl Pts',(17.4439818599249,-20.6306016164573,
17.1744763053273));
#179495=CARTESIAN_POINT('Ctrl Pts',(17.4339379676857,-20.6228347964638,
17.1752227885969));
#179496=CARTESIAN_POINT('Ctrl Pts',(17.3996937386464,-20.5958583930604,
17.1777679174922));
#179497=CARTESIAN_POINT('Ctrl Pts',(17.3758434070302,-20.5762088770927,
17.1795406027697));
#179498=CARTESIAN_POINT('Ctrl Pts',(17.2566649370767,-20.4735599519278,
17.1884481052951));
#179499=CARTESIAN_POINT('Ctrl Pts',(17.168471074874,-20.3826599018042,17.1952181982076));
#179500=CARTESIAN_POINT('Ctrl Pts',(17.0582611819491,-20.2465885634445,
17.2047514608429));
#179501=CARTESIAN_POINT('Ctrl Pts',(17.0289287054711,-20.2077037028477,
17.207414428955));
#179502=CARTESIAN_POINT('Ctrl Pts',(16.9490752892469,-20.0938823813317,
17.2151111645563));
#179503=CARTESIAN_POINT('Ctrl Pts',(16.9019802721141,-20.0166841986583,
17.2202202571225));
#179504=CARTESIAN_POINT('Ctrl Pts',(16.8535788962364,-19.9245707345212,
17.2263207580136));
#179505=CARTESIAN_POINT('Ctrl Pts',(16.8473133867772,-19.9123598134969,
17.2271294148033));
#179506=CARTESIAN_POINT('Ctrl Pts',(16.8374546784434,-19.8926771824009,
17.2284331886303));
#179507=CARTESIAN_POINT('Ctrl Pts',(16.833785805529,-19.8852436607635,17.2289256531454));
#179508=CARTESIAN_POINT('Ctrl Pts',(16.8273484107973,-19.8720054750239,
17.2298028772209));
#179509=CARTESIAN_POINT('Ctrl Pts',(16.8245624875533,-19.866209353122,17.2301870246928));
#179510=CARTESIAN_POINT('Ctrl Pts',(16.8188122844454,-19.8541050898976,
17.2309894394178));
#179511=CARTESIAN_POINT('Ctrl Pts',(16.8158526654903,-19.8477948316081,
17.231407862504));
#179512=CARTESIAN_POINT('Ctrl Pts',(16.8082461371726,-19.8313662678132,
17.2324975416901));
#179513=CARTESIAN_POINT('Ctrl Pts',(16.8036478411164,-19.8212258098082,
17.2331704632612));
#179514=CARTESIAN_POINT('Ctrl Pts',(16.784012823794,-19.7770011164761,17.2361069458593));
#179515=CARTESIAN_POINT('Ctrl Pts',(16.7697980192573,-19.7425612764889,
17.2383983247988));
#179516=CARTESIAN_POINT('Ctrl Pts',(16.7344380958012,-19.6500402388165,
17.2445700205905));
#179517=CARTESIAN_POINT('Ctrl Pts',(16.7149163225501,-19.5913809174453,
17.2485002146646));
#179518=CARTESIAN_POINT('Ctrl Pts',(16.6441980815093,-19.3431153339715,
17.2651780990222));
#179519=CARTESIAN_POINT('Ctrl Pts',(16.6169468519359,-19.1477387709714,
17.2785137881608));
#179520=CARTESIAN_POINT('Ctrl Pts',(16.6170000778107,-18.9514260221329,
17.2909082085163));
#179521=CARTESIAN_POINT('Ctrl Pts',(16.6170000784481,-18.9514236762823,
17.290908356624));
#179522=CARTESIAN_POINT('Ctrl Pts',(16.6170043638442,-18.9356822047961,
17.2919022109546));
#179523=CARTESIAN_POINT('Ctrl Pts',(16.6171842237133,-18.9199407054316,
17.292888940478));
#179524=CARTESIAN_POINT('Ctrl Pts',(16.6177851449884,-18.8933322805094,
17.2945431869397));
#179525=CARTESIAN_POINT('Ctrl Pts',(16.6181143695764,-18.8824642249398,
17.2952149993387));
#179526=CARTESIAN_POINT('Ctrl Pts',(16.6187085001638,-18.8668317574946,
17.2961753157442));
#179527=CARTESIAN_POINT('Ctrl Pts',(16.6189057980431,-18.8620651532563,
17.2964673281209));
#179528=CARTESIAN_POINT('Ctrl Pts',(16.6192791185133,-18.8537280713092,
17.2969766202679));
#179529=CARTESIAN_POINT('Ctrl Pts',(16.6194480741293,-18.8501573184082,
17.2971942817453));
#179530=CARTESIAN_POINT('Ctrl Pts',(16.6197955281146,-18.8431880877566,
17.2976181686609));
#179531=CARTESIAN_POINT('Ctrl Pts',(16.6199731786413,-18.8397895708806,
17.297824440825));
#179532=CARTESIAN_POINT('Ctrl Pts',(16.620344944467,-18.832992030622,17.2982361298109));
#179533=CARTESIAN_POINT('Ctrl Pts',(16.6205390638674,-18.8295930460491,
17.2984415466401));
#179534=CARTESIAN_POINT('Ctrl Pts',(16.6210263182057,-18.8214082324557,
17.2989351641012));
#179535=CARTESIAN_POINT('Ctrl Pts',(16.6213275158666,-18.8166228766968,
17.2992229156209));
#179536=CARTESIAN_POINT('Ctrl Pts',(16.6224923795772,-18.7990673690464,
17.300275579228));
#179537=CARTESIAN_POINT('Ctrl Pts',(16.6234556132615,-18.7863038009819,
17.3010351230314));
#179538=CARTESIAN_POINT('Ctrl Pts',(16.6267051710482,-18.7478907611317,
17.3033056967415));
#179539=CARTESIAN_POINT('Ctrl Pts',(16.6293438413026,-18.7222726522791,
17.3047993492989));
#179540=CARTESIAN_POINT('Ctrl Pts',(16.6519756108748,-18.5359691574001,
17.3155522149559));
#179541=CARTESIAN_POINT('Ctrl Pts',(16.6898786703323,-18.3779977387511,
17.324109604356));
#179542=CARTESIAN_POINT('Ctrl Pts',(16.7454193703768,-18.2258897607889,
17.3329785739071));
#179543=CARTESIAN_POINT('Origin',(18.734,-18.952,0.));
#179544=CARTESIAN_POINT('',(16.7454193588142,-18.2258897924551,18.356854558525));
#179545=CARTESIAN_POINT('',(16.7454193851305,-18.225889720383,18.1318062882837));
#179546=CARTESIAN_POINT('',(16.7454193692319,-18.2258897639242,0.));
#179547=CARTESIAN_POINT('Ctrl Pts',(16.7454193588142,-18.2258897924551,
18.356854558525));
#179548=CARTESIAN_POINT('Ctrl Pts',(16.7400764561234,-18.2405222721369,
18.3558520701171));
#179549=CARTESIAN_POINT('Ctrl Pts',(16.7348944425785,-18.2552154073299,
18.35484548685));
#179550=CARTESIAN_POINT('Ctrl Pts',(16.6860061191413,-18.3988716263901,
18.3450068903525));
#179551=CARTESIAN_POINT('Ctrl Pts',(16.6546780349517,-18.5317066270795,
18.3359031807386));
#179552=CARTESIAN_POINT('Ctrl Pts',(16.6262469177696,-18.7406855078547,
18.3221216440023));
#179553=CARTESIAN_POINT('Ctrl Pts',(16.6200989575309,-18.8152457073574,
18.3173148331482));
#179554=CARTESIAN_POINT('Ctrl Pts',(16.6176490865155,-18.8988371634596,
18.3121557706889));
#179555=CARTESIAN_POINT('Ctrl Pts',(16.6174451484326,-18.9076937611231,
18.3116120637845));
#179556=CARTESIAN_POINT('Ctrl Pts',(16.6172222392193,-18.9210041511307,
18.3107995602777));
#179557=CARTESIAN_POINT('Ctrl Pts',(16.6171617203416,-18.9254570198558,
18.3105285218209));
#179558=CARTESIAN_POINT('Ctrl Pts',(16.6170816556373,-18.933129653031,18.3100628795151));
#179559=CARTESIAN_POINT('Ctrl Pts',(16.6170554040053,-18.9363492920891,
18.3098679033127));
#179560=CARTESIAN_POINT('Ctrl Pts',(16.6170125976594,-18.943639116196,18.3094273992575));
#179561=CARTESIAN_POINT('Ctrl Pts',(16.6170004354112,-18.9477092868115,
18.3091821201468));
#179562=CARTESIAN_POINT('Ctrl Pts',(16.6169992761218,-18.9588398470706,
18.3085131347873));
#179563=CARTESIAN_POINT('Ctrl Pts',(16.6170338608354,-18.9659002604124,
18.3080907283311));
#179564=CARTESIAN_POINT('Ctrl Pts',(16.6174008059016,-19.0029597443722,
18.3058831704996));
#179565=CARTESIAN_POINT('Ctrl Pts',(16.6183355231144,-19.0329510574179,
18.3041297180233));
#179566=CARTESIAN_POINT('Ctrl Pts',(16.6230423596418,-19.1226663565822,
18.2989567809465));
#179567=CARTESIAN_POINT('Ctrl Pts',(16.6287092893136,-19.1822633632961,
18.2956161958563));
#179568=CARTESIAN_POINT('Ctrl Pts',(16.6597465950646,-19.4070599465742,
18.2831216880128));
#179569=CARTESIAN_POINT('Ctrl Pts',(16.7021117943599,-19.5692828192729,
18.274274328893));
#179570=CARTESIAN_POINT('Ctrl Pts',(16.7847365639451,-19.7799918556394,
18.2615097814227));
#179571=CARTESIAN_POINT('Ctrl Pts',(16.8086669656977,-19.8342075908473,
18.2581084339116));
#179572=CARTESIAN_POINT('Ctrl Pts',(16.840246159529,-19.898327240206,18.2539094836516));
#179573=CARTESIAN_POINT('Ctrl Pts',(16.8457498264668,-19.9092617858095,
18.2531871018665));
#179574=CARTESIAN_POINT('Ctrl Pts',(16.8549745014493,-19.9272000109042,
18.251991292269));
#179575=CARTESIAN_POINT('Ctrl Pts',(16.8586406286716,-19.9342316993587,
18.2515197954675));
#179576=CARTESIAN_POINT('Ctrl Pts',(16.865323900166,-19.946876496004,18.2506668833291));
#179577=CARTESIAN_POINT('Ctrl Pts',(16.868327058848,-19.9524969183725,18.2502859672664));
#179578=CARTESIAN_POINT('Ctrl Pts',(16.8748002255645,-19.9644809801034,
18.2494698479992));
#179579=CARTESIAN_POINT('Ctrl Pts',(16.8782776236858,-19.9708405156567,
18.2490343845758));
#179580=CARTESIAN_POINT('Ctrl Pts',(16.8877882472654,-19.9880235085378,
18.2478512706386));
#179581=CARTESIAN_POINT('Ctrl Pts',(16.8938838843996,-19.9988119301249,
18.24710138825));
#179582=CARTESIAN_POINT('Ctrl Pts',(16.9256761857397,-20.0539440310081,
18.2432323067795));
#179583=CARTESIAN_POINT('Ctrl Pts',(16.9528804660932,-20.0973943243011,
18.2400587086051));
#179584=CARTESIAN_POINT('Ctrl Pts',(17.0774362911812,-20.2811502978823,
18.2260766991341));
#179585=CARTESIAN_POINT('Ctrl Pts',(17.1899783146709,-20.4103635560819,
18.2147047805777));
#179586=CARTESIAN_POINT('Ctrl Pts',(17.3851539398323,-20.5862502501211,
18.1974264899812));
#179587=CARTESIAN_POINT('Ctrl Pts',(17.4574774253475,-20.643346703788,18.1914504276524));
#179588=CARTESIAN_POINT('Ctrl Pts',(17.5412586625768,-20.701042761103,18.1851656348704));
#179589=CARTESIAN_POINT('Ctrl Pts',(17.5492592032924,-20.7064719236629,
18.1845715961144));
#179590=CARTESIAN_POINT('Ctrl Pts',(17.5611326974641,-20.7144110141467,
18.1836993211302));
#179591=CARTESIAN_POINT('Ctrl Pts',(17.5649769819699,-20.7169633073778,
18.183418336287));
#179592=CARTESIAN_POINT('Ctrl Pts',(17.5718145255215,-20.7214707413266,
18.1829211495414));
#179593=CARTESIAN_POINT('Ctrl Pts',(17.5748044194671,-20.7234308872347,
18.1827046145));
#179594=CARTESIAN_POINT('Ctrl Pts',(17.5812240289241,-20.7276163083607,
18.1822415689968));
#179595=CARTESIAN_POINT('Ctrl Pts',(17.5846552194365,-20.7298392194033,
18.1819952159324));
#179596=CARTESIAN_POINT('Ctrl Pts',(17.5940985110213,-20.7359183305948,
18.1813202637702));
#179597=CARTESIAN_POINT('Ctrl Pts',(17.6001237855358,-20.7397541073622,
18.1808930036154));
#179598=CARTESIAN_POINT('Ctrl Pts',(17.6325054773727,-20.7601391942149,
18.1786142384344));
#179599=CARTESIAN_POINT('Ctrl Pts',(17.6592064858268,-20.7761372377348,
18.1767969117996));
#179600=CARTESIAN_POINT('Ctrl Pts',(17.8286695253085,-20.8726583177353,
18.1655817017695));
#179601=CARTESIAN_POINT('Ctrl Pts',(17.9800402216489,-20.9369706988151,
18.1569209978717));
#179602=CARTESIAN_POINT('Ctrl Pts',(18.2497879157544,-21.0162106765199,
18.1415316232652));
#179603=CARTESIAN_POINT('Ctrl Pts',(18.3647797420225,-21.0398453399555,
18.1349895654155));
#179604=CARTESIAN_POINT('Ctrl Pts',(18.4953200974181,-21.0555506284855,
18.1272869755072));
#179605=CARTESIAN_POINT('Ctrl Pts',(18.5095292563648,-21.0571142992307,
18.1264451805726));
#179606=CARTESIAN_POINT('Ctrl Pts',(18.5321672418979,-21.0593737314639,
18.1250982272442));
#179607=CARTESIAN_POINT('Ctrl Pts',(18.5405864377595,-21.0601631096962,
18.1245960126324));
#179608=CARTESIAN_POINT('Ctrl Pts',(18.5554424106275,-21.0614662549967,
18.1237075023239));
#179609=CARTESIAN_POINT('Ctrl Pts',(18.5618772682622,-21.062001056276,18.1233218731251));
#179610=CARTESIAN_POINT('Ctrl Pts',(18.5751908607504,-21.0630462416032,
18.1225223782265));
#179611=CARTESIAN_POINT('Ctrl Pts',(18.5820698370767,-21.0635524622274,
18.1221083864093));
#179612=CARTESIAN_POINT('Ctrl Pts',(18.5997320080844,-21.0647654584667,
18.1210430678004));
#179613=CARTESIAN_POINT('Ctrl Pts',(18.6105182650633,-21.0654232965734,
18.1203902125689));
#179614=CARTESIAN_POINT('Ctrl Pts',(18.6555453131005,-21.0678235566071,
18.1176551284641));
#179615=CARTESIAN_POINT('Ctrl Pts',(18.6898192841759,-21.0688165506296,
18.1155495890787));
#179616=CARTESIAN_POINT('Ctrl Pts',(18.7791606103171,-21.0692343218607,
18.1099963704284));
#179617=CARTESIAN_POINT('Ctrl Pts',(18.8342054418855,-21.0673436375107,
18.1065103274133));
#179618=CARTESIAN_POINT('Ctrl Pts',(18.9981749486223,-21.05529737631,18.09594279428));
#179619=CARTESIAN_POINT('Ctrl Pts',(19.1064471683049,-21.0388463998676,
18.0887129066814));
#179620=CARTESIAN_POINT('Ctrl Pts',(19.2565111520279,-21.0039918660478,
18.0785361397149));
#179621=CARTESIAN_POINT('Ctrl Pts',(19.2997372543213,-20.9924975024954,
18.0755876314039));
#179622=CARTESIAN_POINT('Ctrl Pts',(19.3667237620158,-20.9723924665874,
18.071017384995));
#179623=CARTESIAN_POINT('Ctrl Pts',(19.3907490064471,-20.9647110799636,
18.0693780886127));
#179624=CARTESIAN_POINT('Ctrl Pts',(19.461861411588,-20.9405659528622,18.0645357239251));
#179625=CARTESIAN_POINT('Ctrl Pts',(19.5085137468885,-20.9228643042607,
18.0613716945036));
#179626=CARTESIAN_POINT('Ctrl Pts',(19.5617050572443,-20.9005005550611,
18.0578132669912));
#179627=CARTESIAN_POINT('Ctrl Pts',(19.568892553094,-20.8974317011809,18.0573334962332));
#179628=CARTESIAN_POINT('Ctrl Pts',(19.5803423593787,-20.8924678212796,
18.0565711066511));
#179629=CARTESIAN_POINT('Ctrl Pts',(19.584615607449,-20.8905984225786,18.0562869942557));
#179630=CARTESIAN_POINT('Ctrl Pts',(19.5921674256897,-20.8872649847555,
18.0557856979716));
#179631=CARTESIAN_POINT('Ctrl Pts',(19.5954484924717,-20.8858067088761,
18.055568166356));
#179632=CARTESIAN_POINT('Ctrl Pts',(19.6023887945438,-20.8827009103173,
18.0551086141341));
#179633=CARTESIAN_POINT('Ctrl Pts',(19.6060470528497,-20.8810513320856,
18.0548667219678));
#179634=CARTESIAN_POINT('Ctrl Pts',(19.6158937875347,-20.8765775173519,
18.0542164921772));
#179635=CARTESIAN_POINT('Ctrl Pts',(19.6220734394534,-20.8737338113788,
18.0538093345541));
#179636=CARTESIAN_POINT('Ctrl Pts',(19.6524932152291,-20.8595573958998,
18.0518090854611));
#179637=CARTESIAN_POINT('Ctrl Pts',(19.6765318660155,-20.8477950409794,
18.0502410366366));
#179638=CARTESIAN_POINT('Ctrl Pts',(19.7451561995693,-20.81258835296,18.0457830247411));
#179639=CARTESIAN_POINT('Ctrl Pts',(19.7891384359692,-20.7880036592014,
18.0429484655315));
#179640=CARTESIAN_POINT('Ctrl Pts',(19.9451426672729,-20.6933425118803,
18.0328291654504));
#179641=CARTESIAN_POINT('Ctrl Pts',(20.0514209257145,-20.6143913048451,
18.0257917938663));
#179642=CARTESIAN_POINT('Ctrl Pts',(20.2269455796162,-20.456529724716,18.0128052365207));
#179643=CARTESIAN_POINT('Ctrl Pts',(20.2990060227302,-20.381422366323,18.0069649199435));
#179644=CARTESIAN_POINT('Ctrl Pts',(20.3742145569046,-20.2905002207869,
18.0000501829558));
#179645=CARTESIAN_POINT('Ctrl Pts',(20.3830666934791,-20.2795788714724,
17.999222132289));
#179646=CARTESIAN_POINT('Ctrl Pts',(20.3970253758706,-20.2620022698628,
17.9978930734479));
#179647=CARTESIAN_POINT('Ctrl Pts',(20.4022023703073,-20.2554033130414,
17.9973948865358));
#179648=CARTESIAN_POINT('Ctrl Pts',(20.4112884544689,-20.2436787491711,
17.9965110564187));
#179649=CARTESIAN_POINT('Ctrl Pts',(20.4152136257635,-20.2385656973833,
17.9961260571739));
#179650=CARTESIAN_POINT('Ctrl Pts',(20.4233078818155,-20.2279215704402,
17.9953254445956));
#179651=CARTESIAN_POINT('Ctrl Pts',(20.4274732910753,-20.2223878085526,
17.9949096931681));
#179652=CARTESIAN_POINT('Ctrl Pts',(20.4381457778705,-20.2080636054719,
17.9938346876592));
#179653=CARTESIAN_POINT('Ctrl Pts',(20.4446119661486,-20.1992430827485,
17.9931738511512));
#179654=CARTESIAN_POINT('Ctrl Pts',(20.4717394018219,-20.1616307773585,
17.9903603677151));
#179655=CARTESIAN_POINT('Ctrl Pts',(20.4917433502846,-20.1323740603814,
17.988182706553));
#179656=CARTESIAN_POINT('Ctrl Pts',(20.5423282426543,-20.0542521105974,
17.982392237566));
#179657=CARTESIAN_POINT('Ctrl Pts',(20.5716626651955,-20.0046185190729,
17.9787368537524));
#179658=CARTESIAN_POINT('Ctrl Pts',(20.6747978948891,-19.812633956754,17.9647006140863));
#179659=CARTESIAN_POINT('Ctrl Pts',(20.7343682062156,-19.6632713748046,
17.9539384240938));
#179660=CARTESIAN_POINT('Ctrl Pts',(20.7802679302856,-19.4948449269851,
17.9425841917919));
#179661=CARTESIAN_POINT('Ctrl Pts',(20.7838843496348,-19.4810247860628,
17.941658449567));
#179662=CARTESIAN_POINT('Ctrl Pts',(20.7893293716988,-19.4593220110097,
17.9402149344421));
#179663=CARTESIAN_POINT('Ctrl Pts',(20.7912531015821,-19.4514638405245,
17.9396943574825));
#179664=CARTESIAN_POINT('Ctrl Pts',(20.8031618681265,-19.4015818605624,
17.9364038514231));
#179665=CARTESIAN_POINT('Ctrl Pts',(20.8119046449392,-19.3592684119933,
17.9336753441514));
#179666=CARTESIAN_POINT('Ctrl Pts',(20.8206391076489,-19.3093268433427,
17.9305508082306));
#179667=CARTESIAN_POINT('Ctrl Pts',(20.8218918270728,-19.3019327947099,
17.9300906599337));
#179668=CARTESIAN_POINT('Ctrl Pts',(20.8238528448074,-19.2899725369792,
17.9293504768193));
#179669=CARTESIAN_POINT('Ctrl Pts',(20.8245855183514,-19.2854104678857,
17.9290691139141));
#179670=CARTESIAN_POINT('Ctrl Pts',(20.8258587018256,-19.2773136296906,
17.9285715093585));
#179671=CARTESIAN_POINT('Ctrl Pts',(20.8264051975035,-19.2737798567443,
17.9283549324757));
#179672=CARTESIAN_POINT('Ctrl Pts',(20.8275567517551,-19.2662066352444,
17.9278920752393));
#179673=CARTESIAN_POINT('Ctrl Pts',(20.8281590729452,-19.2621668265642,
17.9276459508316));
#179674=CARTESIAN_POINT('Ctrl Pts',(20.8297799980859,-19.2510751824092,
17.9269722700017));
#179675=CARTESIAN_POINT('Ctrl Pts',(20.8307747101782,-19.2440198334942,
17.9265460441383));
#179676=CARTESIAN_POINT('Ctrl Pts',(20.8358902188534,-19.2063619344694,
17.9242826813485));
#179677=CARTESIAN_POINT('Ctrl Pts',(20.8393769454466,-19.1756752769556,
17.9224791780782));
#179678=CARTESIAN_POINT('Ctrl Pts',(20.8478921652947,-19.0826234025755,
17.9171042078029));
#179679=CARTESIAN_POINT('Ctrl Pts',(20.8508293052481,-19.020098421261,17.9136190929229));
#179680=CARTESIAN_POINT('Ctrl Pts',(20.8513435470224,-18.8232739646198,
17.9028009703775));
#179681=CARTESIAN_POINT('Ctrl Pts',(20.838922338549,-18.689289591568,17.8956413110103));
#179682=CARTESIAN_POINT('Ctrl Pts',(20.8063008072433,-18.5173525007892,
17.885930685782));
#179683=CARTESIAN_POINT('Ctrl Pts',(20.7975521954345,-18.4775517128178,
17.8836471978451));
#179684=CARTESIAN_POINT('Ctrl Pts',(20.7757746400694,-18.3905355966297,
17.8785505438787));
#179685=CARTESIAN_POINT('Ctrl Pts',(20.7622451211399,-18.3434713306558,
17.8757248687069));
#179686=CARTESIAN_POINT('Ctrl Pts',(20.7431874442101,-18.284905961505,17.872102839793));
#179687=CARTESIAN_POINT('Ctrl Pts',(20.7391702955488,-18.272926574217,17.8713563295306));
#179688=CARTESIAN_POINT('Ctrl Pts',(20.7326385841842,-18.2540120232031,
17.8701684105764));
#179689=CARTESIAN_POINT('Ctrl Pts',(20.7301945530111,-18.2470526896566,
17.8697293400971));
#179690=CARTESIAN_POINT('Ctrl Pts',(20.7255751912979,-18.2341158036487,
17.8689093634801));
#179691=CARTESIAN_POINT('Ctrl Pts',(20.7234091864662,-18.2281349922804,
17.8685287715346));
#179692=CARTESIAN_POINT('Ctrl Pts',(20.7185415086301,-18.2148811520463,
17.8676819566234));
#179693=CARTESIAN_POINT('Ctrl Pts',(20.7158267510827,-18.2076130564834,
17.8672153003799));
#179694=CARTESIAN_POINT('Ctrl Pts',(20.7078319260588,-18.1865626361052,
17.8658570104972));
#179695=CARTESIAN_POINT('Ctrl Pts',(20.7024476855498,-18.1728206096663,
17.8649618939631));
#179696=CARTESIAN_POINT('Ctrl Pts',(20.6590069999302,-18.0652729936997,
17.8578889607705));
#179697=CARTESIAN_POINT('Ctrl Pts',(20.6144157506655,-17.9742637670155,
17.8514877320934));
#179698=CARTESIAN_POINT('Ctrl Pts',(20.4930092039418,-17.765746095288,17.8358363724378));
#179699=CARTESIAN_POINT('Ctrl Pts',(20.4106900314191,-17.6519928230237,
17.8264608633022));
#179700=CARTESIAN_POINT('Ctrl Pts',(20.3067311664855,-17.5347910863474,
17.8162460962281));
#179701=CARTESIAN_POINT('Ctrl Pts',(20.2955726167858,-17.5225051906479,
17.8151681766725));
#179702=CARTESIAN_POINT('Ctrl Pts',(20.2480212819138,-17.4713710638967,
17.8106556317554));
#179703=CARTESIAN_POINT('Ctrl Pts',(20.2103112464261,-17.4337679284982,
17.8072720231526));
#179704=CARTESIAN_POINT('Ctrl Pts',(20.164822881924,-17.391708104282,17.8034503206394));
#179705=CARTESIAN_POINT('Ctrl Pts',(20.1583887795724,-17.3858322152769,
17.8029155386089));
#179706=CARTESIAN_POINT('Ctrl Pts',(20.148590524906,-17.3769943706839,17.8021100935373));
#179707=CARTESIAN_POINT('Ctrl Pts',(20.1452530339559,-17.3740031810754,
17.801837297632));
#179708=CARTESIAN_POINT('Ctrl Pts',(20.1392445749264,-17.3686524748473,
17.8013490110623));
#179709=CARTESIAN_POINT('Ctrl Pts',(20.1365771372497,-17.3662890946283,
17.8011332327703));
#179710=CARTESIAN_POINT('Ctrl Pts',(20.130767376258,-17.3611677094757,17.8006654229155));
#179711=CARTESIAN_POINT('Ctrl Pts',(20.1276228571509,-17.3584122827174,
17.8004135827683));
#179712=CARTESIAN_POINT('Ctrl Pts',(20.1187653325902,-17.3506970270839,
17.7997079411251));
#179713=CARTESIAN_POINT('Ctrl Pts',(20.1130338065887,-17.3457584236439,
17.7992556880434));
#179714=CARTESIAN_POINT('Ctrl Pts',(20.0785729936607,-17.3163854799728,
17.7965615891902));
#179715=CARTESIAN_POINT('Ctrl Pts',(20.0492194797488,-17.2926900501522,
17.7943703755856));
#179716=CARTESIAN_POINT('Ctrl Pts',(19.9504458439372,-17.2172247554472,
17.7872726040437));
#179717=CARTESIAN_POINT('Ctrl Pts',(19.8784794425841,-17.1689254594074,
17.7825305768209));
#179718=CARTESIAN_POINT('Ctrl Pts',(19.6518050088679,-17.0361900637981,
17.7682366619213));
#179719=CARTESIAN_POINT('Ctrl Pts',(19.4893704272039,-16.9665271114053,
17.7587731110688));
#179720=CARTESIAN_POINT('Ctrl Pts',(19.2981408099133,-16.9114214610588,
17.7472083749291));
#179721=CARTESIAN_POINT('Ctrl Pts',(19.2759885527132,-16.9054262839702,
17.745863894274));
#179722=CARTESIAN_POINT('Ctrl Pts',(19.2444966582213,-16.8974506195116,
17.7439440442451));
#179723=CARTESIAN_POINT('Ctrl Pts',(19.2352338795538,-16.8951712301748,
17.7433783224094));
#179724=CARTESIAN_POINT('Ctrl Pts',(19.2201538561888,-16.8915682451773,
17.7424555202888));
#179725=CARTESIAN_POINT('Ctrl Pts',(19.2143457991763,-16.890206484572,17.7420996732026));
#179726=CARTESIAN_POINT('Ctrl Pts',(19.2021723961485,-16.8874065307825,
17.7413529006346));
#179727=CARTESIAN_POINT('Ctrl Pts',(19.1958060094738,-16.8859731865765,
17.740961823602));
#179728=CARTESIAN_POINT('Ctrl Pts',(19.1806378159044,-16.8826317936806,
17.7400287516068));
#179729=CARTESIAN_POINT('Ctrl Pts',(19.1718303136823,-16.8807504437117,
17.7394859070532));
#179730=CARTESIAN_POINT('Ctrl Pts',(19.1420842674372,-16.8745946660899,
17.7376488428849));
#179731=CARTESIAN_POINT('Ctrl Pts',(19.1210936109959,-16.8705812111768,
17.7363463344652));
#179732=CARTESIAN_POINT('Ctrl Pts',(19.0709954331502,-16.8617863637605,
17.7332220376431));
#179733=CARTESIAN_POINT('Ctrl Pts',(19.0418422794558,-16.8572943016439,
17.7313914479273));
#179734=CARTESIAN_POINT('Ctrl Pts',(18.8436279823292,-16.8309796108381,
17.7188582851884));
#179735=CARTESIAN_POINT('Ctrl Pts',(18.6725798007028,-16.8290408593784,
17.7075426535115));
#179736=CARTESIAN_POINT('Ctrl Pts',(18.4039839765343,-16.8585009795282,
17.689739829831));
#179737=CARTESIAN_POINT('Ctrl Pts',(18.3056615492848,-16.876384518382,17.683234611176));
#179738=CARTESIAN_POINT('Ctrl Pts',(18.1995667849229,-16.9035459200741,
17.6764681908364));
#179739=CARTESIAN_POINT('Ctrl Pts',(18.1901918094478,-16.9060147510222,
17.6758725433633));
#179740=CARTESIAN_POINT('Ctrl Pts',(18.1763750406761,-16.9097549747216,
17.6749983664912));
#179741=CARTESIAN_POINT('Ctrl Pts',(18.1719200731995,-16.9109766058771,
17.6747170715071));
#179742=CARTESIAN_POINT('Ctrl Pts',(18.1640238597279,-16.9131697018239,
17.6742195420543));
#179743=CARTESIAN_POINT('Ctrl Pts',(18.1605810440586,-16.9141353119289,
17.6740029727291));
#179744=CARTESIAN_POINT('Ctrl Pts',(18.1532100918069,-16.9162228091859,
17.6735400818566));
#179745=CARTESIAN_POINT('Ctrl Pts',(18.1492827620527,-16.9173473415853,
17.6732939165151));
#179746=CARTESIAN_POINT('Ctrl Pts',(18.1385116718984,-16.9204652449808,
17.6726200081316));
#179747=CARTESIAN_POINT('Ctrl Pts',(18.1316746130291,-16.9224818450536,
17.6721935971473));
#179748=CARTESIAN_POINT('Ctrl Pts',(18.0952336816106,-16.933430518794,17.6699274868392));
#179749=CARTESIAN_POINT('Ctrl Pts',(18.0658163244966,-16.9429763658007,
17.6681215180021));
#179750=CARTESIAN_POINT('Ctrl Pts',(17.9774217710695,-16.9738167432209,
17.6627364893235));
#179751=CARTESIAN_POINT('Ctrl Pts',(17.9191687176525,-16.997090604706,17.6592441620421));
#179752=CARTESIAN_POINT('Ctrl Pts',(17.7219681153042,-17.0862277143227,
17.647350561704));
#179753=CARTESIAN_POINT('Ctrl Pts',(17.5892207147139,-17.1646008704155,
17.6391831950194));
#179754=CARTESIAN_POINT('Ctrl Pts',(17.4622383317729,-17.2595654092346,
17.6302908518846));
#179755=CARTESIAN_POINT('Ctrl Pts',(17.4583592365505,-17.2624872811987,
17.6300181201842));
#179756=CARTESIAN_POINT('Ctrl Pts',(17.4040578853205,-17.3036826054145,
17.6261847470864));
#179757=CARTESIAN_POINT('Ctrl Pts',(17.3553710716627,-17.3441824037655,
17.6225575686703));
#179758=CARTESIAN_POINT('Ctrl Pts',(17.2993260861164,-17.3952224825379,
17.6181059983586));
#179759=CARTESIAN_POINT('Ctrl Pts',(17.2901524789185,-17.4037268316399,
17.6173680341071));
#179760=CARTESIAN_POINT('Ctrl Pts',(17.2752275868538,-17.4178108839172,
17.6161517061893));
#179761=CARTESIAN_POINT('Ctrl Pts',(17.2694315774682,-17.4233428997032,
17.6156753909468));
#179762=CARTESIAN_POINT('Ctrl Pts',(17.2590771665387,-17.433338636389,17.6148172408564));
#179763=CARTESIAN_POINT('Ctrl Pts',(17.254507253845,-17.4377903333131,17.6144359323341));
#179764=CARTESIAN_POINT('Ctrl Pts',(17.2456933740911,-17.4464542051588,
17.6136954856038));
#179765=CARTESIAN_POINT('Ctrl Pts',(17.24144698857,-17.450663841767,17.6133364610283));
#179766=CARTESIAN_POINT('Ctrl Pts',(17.2299424509366,-17.4621658654195,
17.6123574797289));
#179767=CARTESIAN_POINT('Ctrl Pts',(17.2227196055798,-17.4694931962907,
17.6117359722909));
#179768=CARTESIAN_POINT('Ctrl Pts',(17.1934253779375,-17.4996477505744,
17.6091867183149));
#179769=CARTESIAN_POINT('Ctrl Pts',(17.1718164019722,-17.5229165675612,
17.6072390961125));
#179770=CARTESIAN_POINT('Ctrl Pts',(17.1176161436062,-17.5839788094522,
17.6021745282846));
#179771=CARTESIAN_POINT('Ctrl Pts',(17.0858244741928,-17.622452872298,17.5990267722717));
#179772=CARTESIAN_POINT('Ctrl Pts',(17.0102418961657,-17.7208034929502,
17.5910887415768));
#179773=CARTESIAN_POINT('Ctrl Pts',(16.9681834221041,-17.7819242594128,
17.586247892214));
#179774=CARTESIAN_POINT('Ctrl Pts',(16.855520092246,-17.9656028583405,17.5720554976599));
#179775=CARTESIAN_POINT('Ctrl Pts',(16.7938830445993,-18.0931634557097,
17.5626092881251));
#179776=CARTESIAN_POINT('Ctrl Pts',(16.7454193574352,-18.2258897962317,
17.5536949220328));
#179777=CARTESIAN_POINT('Ctrl Pts',(16.7454193703768,-18.2258897607889,
17.3329785739071));
#179778=CARTESIAN_POINT('Ctrl Pts',(16.7466515045255,-18.2225153446616,
17.333175326203));
#179779=CARTESIAN_POINT('Ctrl Pts',(16.7478923195581,-18.2191438132461,
17.333372211731));
#179780=CARTESIAN_POINT('Ctrl Pts',(16.7755868005906,-18.1444796378743,
17.3377392514039));
#179781=CARTESIAN_POINT('Ctrl Pts',(16.8058521666827,-18.074665433262,17.3419652870829));
#179782=CARTESIAN_POINT('Ctrl Pts',(16.8590249439553,-17.96812504875,17.3487665315314));
#179783=CARTESIAN_POINT('Ctrl Pts',(16.8794133282801,-17.9302127035193,
17.3512600777808));
#179784=CARTESIAN_POINT('Ctrl Pts',(16.9067979234565,-17.882814048789,17.3544842221763));
#179785=CARTESIAN_POINT('Ctrl Pts',(16.9127377637891,-17.8727271496805,
17.3551766433149));
#179786=CARTESIAN_POINT('Ctrl Pts',(16.9224123738061,-17.8566052618435,
17.3562937204443));
#179787=CARTESIAN_POINT('Ctrl Pts',(16.926094421276,-17.8505387994598,17.3567164491273));
#179788=CARTESIAN_POINT('Ctrl Pts',(16.9331536611214,-17.8390389088988,
17.3575223994155));
#179789=CARTESIAN_POINT('Ctrl Pts',(16.9365251229351,-17.8336020424348,
17.3579054070299));
#179790=CARTESIAN_POINT('Ctrl Pts',(16.944261717024,-17.821251250412,17.3587800270841));
#179791=CARTESIAN_POINT('Ctrl Pts',(16.9486423462773,-17.8143471963686,
17.3592722101097));
#179792=CARTESIAN_POINT('Ctrl Pts',(16.9601171048081,-17.7964920050116,
17.3605537035385));
#179793=CARTESIAN_POINT('Ctrl Pts',(16.9672725992034,-17.7855808936593,
17.3613452949648));
#179794=CARTESIAN_POINT('Ctrl Pts',(17.0151698612886,-17.7139963283021,
17.3665957660338));
#179795=CARTESIAN_POINT('Ctrl Pts',(17.0589249661821,-17.6554076387175,
17.3711685695935));
#179796=CARTESIAN_POINT('Ctrl Pts',(17.2322419388608,-17.4467832936557,
17.3885131931583));
#179797=CARTESIAN_POINT('Ctrl Pts',(17.3796158935411,-17.312920191456,17.4019442721551));
#179798=CARTESIAN_POINT('Ctrl Pts',(17.5667165808522,-17.1856672732093,
17.4164433210276));
#179799=CARTESIAN_POINT('Ctrl Pts',(17.5903146959775,-17.1702968927357,
17.4182290118084));
#179800=CARTESIAN_POINT('Ctrl Pts',(17.6243045917675,-17.1491116261031,
17.4207331565202));
#179801=CARTESIAN_POINT('Ctrl Pts',(17.6344487020055,-17.1429070380755,
17.4214720965235));
#179802=CARTESIAN_POINT('Ctrl Pts',(17.6501569297104,-17.1334801278939,
17.4226028199757));
#179803=CARTESIAN_POINT('Ctrl Pts',(17.6556841793829,-17.1301972336046,
17.4229981334577));
#179804=CARTESIAN_POINT('Ctrl Pts',(17.664878208137,-17.1247929680169,17.4236513618647));
#179805=CARTESIAN_POINT('Ctrl Pts',(17.6685365104961,-17.1226573593757,
17.4239101495242));
#179806=CARTESIAN_POINT('Ctrl Pts',(17.6756376041958,-17.1185404785403,
17.4244102530051));
#179807=CARTESIAN_POINT('Ctrl Pts',(17.6790796072533,-17.116557888886,17.42465165181));
#179808=CARTESIAN_POINT('Ctrl Pts',(17.6855404550577,-17.1128606263513,
17.4251028549123));
#179809=CARTESIAN_POINT('Ctrl Pts',(17.6885579020581,-17.1111437119853,
17.4253127990916));
#179810=CARTESIAN_POINT('Ctrl Pts',(17.6955747901981,-17.1071739502924,
17.4257992113402));
#179811=CARTESIAN_POINT('Ctrl Pts',(17.6995773391968,-17.1049266853319,
17.4260753189192));
#179812=CARTESIAN_POINT('Ctrl Pts',(17.7119250203324,-17.0980467001937,
17.426923047579));
#179813=CARTESIAN_POINT('Ctrl Pts',(17.7202943316885,-17.0934573107749,
17.4274919647424));
#179814=CARTESIAN_POINT('Ctrl Pts',(17.8321453290519,-17.0331031169082,
17.4350237496617));
#179815=CARTESIAN_POINT('Ctrl Pts',(17.9400816610013,-16.9859865882986,
17.4414867714133));
#179816=CARTESIAN_POINT('Ctrl Pts',(18.1551743551717,-16.9127177939142,
17.4538602737133));
#179817=CARTESIAN_POINT('Ctrl Pts',(18.2615520578762,-16.88548042931,17.4597628205106));
#179818=CARTESIAN_POINT('Ctrl Pts',(18.4445804020308,-16.8534943880991,
17.4700911316911));
#179819=CARTESIAN_POINT('Ctrl Pts',(18.5202503258121,-16.8444424532063,
17.4744073521615));
#179820=CARTESIAN_POINT('Ctrl Pts',(18.6151569645426,-16.8382533811421,
17.4799597314741));
#179821=CARTESIAN_POINT('Ctrl Pts',(18.6340908163362,-16.8372738815052,
17.4810741218581));
#179822=CARTESIAN_POINT('Ctrl Pts',(18.6616106321383,-16.8362206089504,
17.4827045319267));
#179823=CARTESIAN_POINT('Ctrl Pts',(18.6701882559294,-16.8359445399092,
17.4832142160233));
#179824=CARTESIAN_POINT('Ctrl Pts',(18.6852186295816,-16.8355522621957,
17.4841100475738));
#179825=CARTESIAN_POINT('Ctrl Pts',(18.6916707133093,-16.8354133896715,
17.4844954798152));
#179826=CARTESIAN_POINT('Ctrl Pts',(18.7041920260279,-16.8352011609536,
17.4852452171841));
#179827=CARTESIAN_POINT('Ctrl Pts',(18.7102611399795,-16.8351244000574,
17.485609411694));
#179828=CARTESIAN_POINT('Ctrl Pts',(18.72475721061,-16.8350034043338,17.4864812235093));
#179829=CARTESIAN_POINT('Ctrl Pts',(18.7331842175177,-16.8349833853972,
17.4869895951325));
#179830=CARTESIAN_POINT('Ctrl Pts',(18.763515990459,-16.8350924347028,17.4888251480344));
#179831=CARTESIAN_POINT('Ctrl Pts',(18.7854177358851,-16.8355111638474,
17.4901613522644));
#179832=CARTESIAN_POINT('Ctrl Pts',(18.9947964672482,-16.8427659744034,
17.5030428288233));
#179833=CARTESIAN_POINT('Ctrl Pts',(19.1805560049646,-16.8741544315639,
17.5154073934769));
#179834=CARTESIAN_POINT('Ctrl Pts',(19.4350194118993,-16.9528811045889,
17.5329896172734));
#179835=CARTESIAN_POINT('Ctrl Pts',(19.5089809406485,-16.9803735673585,
17.5381663683722));
#179836=CARTESIAN_POINT('Ctrl Pts',(19.6139340063293,-17.0262072150448,
17.5454645850971));
#179837=CARTESIAN_POINT('Ctrl Pts',(19.6462636334707,-17.0413097797935,
17.5477054087737));
#179838=CARTESIAN_POINT('Ctrl Pts',(19.6848613524739,-17.0605436533822,
17.5503584071934));
#179839=CARTESIAN_POINT('Ctrl Pts',(19.6915070832152,-17.0638992049767,
17.5508143836669));
#179840=CARTESIAN_POINT('Ctrl Pts',(19.7018338065578,-17.0691819037774,
17.5515214844195));
#179841=CARTESIAN_POINT('Ctrl Pts',(19.705526985108,-17.0710849092871,17.5517740793255));
#179842=CARTESIAN_POINT('Ctrl Pts',(19.7123799698784,-17.0746416556055,
17.5522422196273));
#179843=CARTESIAN_POINT('Ctrl Pts',(19.715541168978,-17.076292492791,17.5524579370719));
#179844=CARTESIAN_POINT('Ctrl Pts',(19.7226966992806,-17.0800522875018,
17.5529457159732));
#179845=CARTESIAN_POINT('Ctrl Pts',(19.7266884516894,-17.082166039391,17.553217469976));
#179846=CARTESIAN_POINT('Ctrl Pts',(19.7385050018084,-17.0884717603059,
17.5540209603089));
#179847=CARTESIAN_POINT('Ctrl Pts',(19.74631034441,-17.0927002469667,17.5545504387007));
#179848=CARTESIAN_POINT('Ctrl Pts',(19.8044399739556,-17.1246661156217,
17.5584859616396));
#179849=CARTESIAN_POINT('Ctrl Pts',(19.8536476315465,-17.1543956803151,
17.561774189942));
#179850=CARTESIAN_POINT('Ctrl Pts',(20.037248612114,-17.2757896791421,17.5741112745422));
#179851=CARTESIAN_POINT('Ctrl Pts',(20.1621260780778,-17.3808220014613,
17.582688730169));
#179852=CARTESIAN_POINT('Ctrl Pts',(20.3154026043149,-17.5432636854615,
17.595054128838));
#179853=CARTESIAN_POINT('Ctrl Pts',(20.3551330743223,-17.5891724486943,
17.5984623859429));
#179854=CARTESIAN_POINT('Ctrl Pts',(20.4156835815707,-17.6655390328142,
17.6040575963685));
#179855=CARTESIAN_POINT('Ctrl Pts',(20.4377764966462,-17.6949451493129,
17.6061954618015));
#179856=CARTESIAN_POINT('Ctrl Pts',(20.4655156953497,-17.7339420225283,
17.6090166814668));
#179857=CARTESIAN_POINT('Ctrl Pts',(20.4718688613332,-17.7430237167468,
17.6096727281285));
#179858=CARTESIAN_POINT('Ctrl Pts',(20.4820942338171,-17.7578877892823,
17.6107451127868));
#179859=CARTESIAN_POINT('Ctrl Pts',(20.4860098085027,-17.7636401844462,
17.6111597949147));
#179860=CARTESIAN_POINT('Ctrl Pts',(20.4934913881546,-17.7747487696926,
17.6119600129509));
#179861=CARTESIAN_POINT('Ctrl Pts',(20.497061477942,-17.7801021256826,17.6123453885218));
#179862=CARTESIAN_POINT('Ctrl Pts',(20.5051884284862,-17.7924096946163,
17.6132308327424));
#179863=CARTESIAN_POINT('Ctrl Pts',(20.5097288172126,-17.7993746097782,
17.6137315116673));
#179864=CARTESIAN_POINT('Ctrl Pts',(20.5217003406142,-17.8179774458804,
17.6150678302696));
#179865=CARTESIAN_POINT('Ctrl Pts',(20.529058746483,-17.8296614844087,17.6159061514545));
#179866=CARTESIAN_POINT('Ctrl Pts',(20.5853756301151,-17.9210549176534,
17.6224569015313));
#179867=CARTESIAN_POINT('Ctrl Pts',(20.6291100596633,-18.0038474687044,
17.6283591228187));
#179868=CARTESIAN_POINT('Ctrl Pts',(20.7242878481568,-18.2171191058028,
17.6434622106105));
#179869=CARTESIAN_POINT('Ctrl Pts',(20.7685233588595,-18.3503307934482,
17.6528245653269));
#179870=CARTESIAN_POINT('Ctrl Pts',(20.8108081481427,-18.5381041227205,
17.6654112154109));
#179871=CARTESIAN_POINT('Ctrl Pts',(20.8204287032005,-18.5897046895771,
17.6688053168593));
#179872=CARTESIAN_POINT('Ctrl Pts',(20.8321550558771,-18.6688200752065,
17.6738624423594));
#179873=CARTESIAN_POINT('Ctrl Pts',(20.8356573148347,-18.6961050864414,
17.6755801270848));
#179874=CARTESIAN_POINT('Ctrl Pts',(20.8393681027406,-18.730276579246,17.6776920510488));
#179875=CARTESIAN_POINT('Ctrl Pts',(20.8400760121589,-18.7371047758992,
17.6781121037737));
#179876=CARTESIAN_POINT('Ctrl Pts',(20.8411464659194,-18.7479436695925,
17.6787756540179));
#179877=CARTESIAN_POINT('Ctrl Pts',(20.841530794977,-18.7519520965744,17.6790203472518));
#179878=CARTESIAN_POINT('Ctrl Pts',(20.8422358736238,-18.7595334588964,
17.679481794289));
#179879=CARTESIAN_POINT('Ctrl Pts',(20.842558974962,-18.7631060679842,17.6796986721527));
#179880=CARTESIAN_POINT('Ctrl Pts',(20.8432791355801,-18.7713012097062,
17.6801948741122));
#179881=CARTESIAN_POINT('Ctrl Pts',(20.843670080889,-18.7759242340723,17.6804738523526));
#179882=CARTESIAN_POINT('Ctrl Pts',(20.8446719124212,-18.7882537333393,
17.6812154689609));
#179883=CARTESIAN_POINT('Ctrl Pts',(20.84525579639,-18.7959624145724,17.6816766336076));
#179884=CARTESIAN_POINT('Ctrl Pts',(20.8491537415796,-18.8514596625095,
17.68497974839));
#179885=CARTESIAN_POINT('Ctrl Pts',(20.8508874253925,-18.8993492732169,
17.6877397177811));
#179886=CARTESIAN_POINT('Ctrl Pts',(20.8510584794881,-18.9757496549838,
17.6920566198715));
#179887=CARTESIAN_POINT('Ctrl Pts',(20.8505471657019,-19.0042383898969,
17.6936472203223));
#179888=CARTESIAN_POINT('Ctrl Pts',(20.847800356483,-19.0762349394366,17.6976371171893));
#179889=CARTESIAN_POINT('Ctrl Pts',(20.8447967734533,-19.1197004703986,
17.7000183932679));
#179890=CARTESIAN_POINT('Ctrl Pts',(20.8295552981277,-19.271827811454,17.7083422034416));
#179891=CARTESIAN_POINT('Ctrl Pts',(20.8102457159763,-19.3796034112313,
17.7142292781981));
#179892=CARTESIAN_POINT('Ctrl Pts',(20.7636353481383,-19.5586256004974,
17.7245156238653));
#179893=CARTESIAN_POINT('Ctrl Pts',(20.7406603971605,-19.630768425109,17.7288049481863));
#179894=CARTESIAN_POINT('Ctrl Pts',(20.7071864373007,-19.7191904556225,
17.7343249090456));
#179895=CARTESIAN_POINT('Ctrl Pts',(20.7002616627995,-19.7367680872222,
17.7354354344716));
#179896=CARTESIAN_POINT('Ctrl Pts',(20.689855121965,-19.7621809578871,17.7370612128874));
#179897=CARTESIAN_POINT('Ctrl Pts',(20.6865594278932,-19.7700917551782,
17.7375701815309));
#179898=CARTESIAN_POINT('Ctrl Pts',(20.6806985941754,-19.7839225972379,
17.7384651852554));
#179899=CARTESIAN_POINT('Ctrl Pts',(20.6781542394562,-19.7898513687653,
17.7388505092289));
#179900=CARTESIAN_POINT('Ctrl Pts',(20.6731622762336,-19.8013383011216,
17.739600354872));
#179901=CARTESIAN_POINT('Ctrl Pts',(20.6707177706073,-19.8068977477676,
17.739964767424));
#179902=CARTESIAN_POINT('Ctrl Pts',(20.6648187837648,-19.8201584339587,
17.7408376157691));
#179903=CARTESIAN_POINT('Ctrl Pts',(20.6613421204035,-19.8278496388554,
17.7413468099521));
#179904=CARTESIAN_POINT('Ctrl Pts',(20.6486422351825,-19.8555029966078,
17.7431883536538));
#179905=CARTESIAN_POINT('Ctrl Pts',(20.6391543619873,-19.8753414067305,
17.7445298030286));
#179906=CARTESIAN_POINT('Ctrl Pts',(20.546150700172,-20.0622662882698,17.7573680597733));
#179907=CARTESIAN_POINT('Ctrl Pts',(20.4411877427197,-20.2177263778437,
17.7696761038217));
#179908=CARTESIAN_POINT('Ctrl Pts',(20.2645491232413,-20.4167207417302,
17.7872412860787));
#179909=CARTESIAN_POINT('Ctrl Pts',(20.2085645656554,-20.4730682112223,
17.792453739437));
#179910=CARTESIAN_POINT('Ctrl Pts',(20.1229116573689,-20.5500914579864,
17.7997953650747));
#179911=CARTESIAN_POINT('Ctrl Pts',(20.0956732934613,-20.5733630359375,
17.8020453620333));
#179912=CARTESIAN_POINT('Ctrl Pts',(20.0620678708746,-20.6006298198979,
17.8047077196299));
#179913=CARTESIAN_POINT('Ctrl Pts',(20.0562551773457,-20.6052954371458,
17.8051642364927));
#179914=CARTESIAN_POINT('Ctrl Pts',(20.0471627086368,-20.612514973446,17.8058719908874));
#179915=CARTESIAN_POINT('Ctrl Pts',(20.0438999142413,-20.6150900431874,
17.8061247033619));
#179916=CARTESIAN_POINT('Ctrl Pts',(20.0378236904137,-20.6198565590691,
17.8065929499846));
#179917=CARTESIAN_POINT('Ctrl Pts',(20.035012334783,-20.6220504849644,17.8068086568785));
#179918=CARTESIAN_POINT('Ctrl Pts',(20.0286295762563,-20.6270055636558,
17.8072962700323));
#179919=CARTESIAN_POINT('Ctrl Pts',(20.0250548865612,-20.6297623963926,
17.8075678697158));
#179920=CARTESIAN_POINT('Ctrl Pts',(20.0144344388798,-20.6378989383835,
17.8083704811578));
#179921=CARTESIAN_POINT('Ctrl Pts',(20.0073635778774,-20.6432459275507,
17.8088992423076));
#179922=CARTESIAN_POINT('Ctrl Pts',(19.9544767104081,-20.6827192962727,
17.8128143714169));
#179923=CARTESIAN_POINT('Ctrl Pts',(19.9073253625779,-20.7150262344839,
17.8160842988135));
#179924=CARTESIAN_POINT('Ctrl Pts',(19.7306682855228,-20.8258361038753,
17.8277759492938));
#179925=CARTESIAN_POINT('Ctrl Pts',(19.5941512185764,-20.8922976198795,
17.8357917844943));
#179926=CARTESIAN_POINT('Ctrl Pts',(19.3644865811762,-20.9750596947134,
17.8492377569215));
#179927=CARTESIAN_POINT('Ctrl Pts',(19.2753073994552,-21.0007233294688,
17.854443600253));
#179928=CARTESIAN_POINT('Ctrl Pts',(19.1641540333276,-21.024944863132,17.8610701470341));
#179929=CARTESIAN_POINT('Ctrl Pts',(19.1435029939371,-21.0291230461215,
17.8623066882897));
#179930=CARTESIAN_POINT('Ctrl Pts',(19.1139908572965,-21.0346368240366,
17.8640828148199));
#179931=CARTESIAN_POINT('Ctrl Pts',(19.1051779063292,-21.0362255517487,
17.8646143392516));
#179932=CARTESIAN_POINT('Ctrl Pts',(19.0899348902619,-21.0388736950105,
17.8655357340878));
#179933=CARTESIAN_POINT('Ctrl Pts',(19.0835094783748,-21.0399594316208,
17.8659247622379));
#179934=CARTESIAN_POINT('Ctrl Pts',(19.0711818117254,-21.0419840054912,
17.8666723923177));
#179935=CARTESIAN_POINT('Ctrl Pts',(19.0652803853635,-21.0429275507541,
17.8670308406058));
#179936=CARTESIAN_POINT('Ctrl Pts',(19.0498904980835,-21.0453213626032,
17.8679670738101));
#179937=CARTESIAN_POINT('Ctrl Pts',(19.0403961078368,-21.0467320960606,
17.8685461059613));
#179938=CARTESIAN_POINT('Ctrl Pts',(19.0078136709391,-21.0513471354881,
17.8705383381295));
#179939=CARTESIAN_POINT('Ctrl Pts',(18.9846831165729,-21.054234579819,17.8719614879708));
#179940=CARTESIAN_POINT('Ctrl Pts',(18.7917146376176,-21.0750933695887,
17.8839119490064));
#179941=CARTESIAN_POINT('Ctrl Pts',(18.6203522476481,-21.0728297787518,
17.8951011276923));
#179942=CARTESIAN_POINT('Ctrl Pts',(18.3616208282738,-21.0379496625969,
17.9123532607126));
#179943=CARTESIAN_POINT('Ctrl Pts',(18.2729391681754,-21.0201579118172,
17.9183162923573));
#179944=CARTESIAN_POINT('Ctrl Pts',(18.1483250731119,-20.986740307303,17.9265592874871));
#179945=CARTESIAN_POINT('Ctrl Pts',(18.111267320365,-20.9757064222499,17.9289921545961));
#179946=CARTESIAN_POINT('Ctrl Pts',(18.0672904376315,-20.9612897757907,
17.9318402829592));
#179947=CARTESIAN_POINT('Ctrl Pts',(18.0600636219527,-20.9588773769331,
17.9323070428516));
#179948=CARTESIAN_POINT('Ctrl Pts',(18.04888037833,-20.955077053035,17.9330271776082));
#179949=CARTESIAN_POINT('Ctrl Pts',(18.0449148704866,-20.9537163288986,
17.9332821102341));
#179950=CARTESIAN_POINT('Ctrl Pts',(18.0375868131264,-20.9511774227121,
17.9337523954949));
#179951=CARTESIAN_POINT('Ctrl Pts',(18.0342232235184,-20.9500025419751,
17.9339679339679));
#179952=CARTESIAN_POINT('Ctrl Pts',(18.0266492252338,-20.9473355192997,
17.9344525573917));
#179953=CARTESIAN_POINT('Ctrl Pts',(18.0224405761324,-20.9458385441875,
17.9347213517472));
#179954=CARTESIAN_POINT('Ctrl Pts',(18.010101128324,-20.9414054772473,17.9355080643364));
#179955=CARTESIAN_POINT('Ctrl Pts',(18.0019834257658,-20.9384328506507,
17.9360238625153));
#179956=CARTESIAN_POINT('Ctrl Pts',(17.9455370956563,-20.9173697215983,
17.9395997087794));
#179957=CARTESIAN_POINT('Ctrl Pts',(17.8978616510936,-20.8975655957638,
17.9425649579697));
#179958=CARTESIAN_POINT('Ctrl Pts',(17.8310733338241,-20.8669127709695,
17.9467037787142));
#179959=CARTESIAN_POINT('Ctrl Pts',(17.8113349880038,-20.8574807284121,
17.9479249836257));
#179960=CARTESIAN_POINT('Ctrl Pts',(17.668446349898,-20.7864598601494,17.956775147596));
#179961=CARTESIAN_POINT('Ctrl Pts',(17.5514174744097,-20.713291793051,17.96409853679));
#179962=CARTESIAN_POINT('Ctrl Pts',(17.3704328114168,-20.5739143045383,
17.9766927937852));
#179963=CARTESIAN_POINT('Ctrl Pts',(17.3021869452797,-20.5139955608119,
17.9817933023191));
#179964=CARTESIAN_POINT('Ctrl Pts',(17.2232621482439,-20.4351702387793,
17.9882924139172));
#179965=CARTESIAN_POINT('Ctrl Pts',(17.2087435238608,-20.4202354887054,
17.9895150355767));
#179966=CARTESIAN_POINT('Ctrl Pts',(17.1883296515957,-20.3986069368003,
17.9912746205168));
#179967=CARTESIAN_POINT('Ctrl Pts',(17.1822523882909,-20.3920860395782,
17.9918037299412));
#179968=CARTESIAN_POINT('Ctrl Pts',(17.1718088761005,-20.3807372962285,
17.992722273466));
#179969=CARTESIAN_POINT('Ctrl Pts',(17.1674233463173,-20.3759273000759,
17.9931108795393));
#179970=CARTESIAN_POINT('Ctrl Pts',(17.1590478684073,-20.3666556501768,
17.993858640533));
#179971=CARTESIAN_POINT('Ctrl Pts',(17.1550545170895,-20.3621971444584,
17.9942176463347));
#179972=CARTESIAN_POINT('Ctrl Pts',(17.1446737499578,-20.3505078313432,
17.9951574325588));
#179973=CARTESIAN_POINT('Ctrl Pts',(17.1383168160314,-20.34325024887,17.9957394788501));
#179974=CARTESIAN_POINT('Ctrl Pts',(17.1165781276013,-20.3180866396199,
17.9977528008678));
#179975=CARTESIAN_POINT('Ctrl Pts',(17.1014468249146,-20.2999674625156,
17.999194311331));
#179976=CARTESIAN_POINT('Ctrl Pts',(16.9829318738435,-20.1531270860759,
18.0108161510283));
#179977=CARTESIAN_POINT('Ctrl Pts',(16.8946445712035,-20.0129890624413,
18.0216100112015));
#179978=CARTESIAN_POINT('Ctrl Pts',(16.7685612740643,-19.7488853971694,
18.0409499369832));
#179979=CARTESIAN_POINT('Ctrl Pts',(16.7241006235977,-19.628968966997,18.0493910386296));
#179980=CARTESIAN_POINT('Ctrl Pts',(16.6875909744737,-19.4942557998273,
18.0580465183784));
#179981=CARTESIAN_POINT('Ctrl Pts',(16.6845683633358,-19.4827176592795,
18.0587812922149));
#179982=CARTESIAN_POINT('Ctrl Pts',(16.6804108697193,-19.4662819679077,
18.0598180364087));
#179983=CARTESIAN_POINT('Ctrl Pts',(16.6791957303449,-19.4614052150545,
18.0601244202281));
#179984=CARTESIAN_POINT('Ctrl Pts',(16.6771318954958,-19.4529948170774,
18.0606506231147));
#179985=CARTESIAN_POINT('Ctrl Pts',(16.6762749145155,-19.4494632442821,
18.0608709160458));
#179986=CARTESIAN_POINT('Ctrl Pts',(16.6746311948224,-19.4426126360486,
18.0612969407393));
#179987=CARTESIAN_POINT('Ctrl Pts',(16.6738433837153,-19.4392939063317,
18.0615027363578));
#179988=CARTESIAN_POINT('Ctrl Pts',(16.671740039967,-19.4303370938981,18.0620565989928));
#179989=CARTESIAN_POINT('Ctrl Pts',(16.6704395975657,-19.4246954468276,
18.0624038044609));
#179990=CARTESIAN_POINT('Ctrl Pts',(16.6657019231818,-19.4037500214372,
18.0636869528289));
#179991=CARTESIAN_POINT('Ctrl Pts',(16.6624115604242,-19.3884130909542,
18.0646148494973));
#179992=CARTESIAN_POINT('Ctrl Pts',(16.6325545372761,-19.2412904073253,
18.073416765317));
#179993=CARTESIAN_POINT('Ctrl Pts',(16.6184239747238,-19.1072739496514,
18.0806878981142));
#179994=CARTESIAN_POINT('Ctrl Pts',(16.6170404620212,-18.9665205574997,
18.0883318251222));
#179995=CARTESIAN_POINT('Ctrl Pts',(16.6170066729076,-18.9602331678495,
18.0886732576158));
#179996=CARTESIAN_POINT('Ctrl Pts',(16.616866854777,-18.8081072288272,18.0969354855539));
#179997=CARTESIAN_POINT('Ctrl Pts',(16.6318021057098,-18.6626640217989,
18.1048962014557));
#179998=CARTESIAN_POINT('Ctrl Pts',(16.6664676958402,-18.4963942861878,
18.1147554600943));
#179999=CARTESIAN_POINT('Ctrl Pts',(16.6717720455133,-18.4729570065316,
18.1161622425507));
#180000=CARTESIAN_POINT('Ctrl Pts',(16.679780444546,-18.4401743679251,18.1181559718257));
#180001=CARTESIAN_POINT('Ctrl Pts',(16.6821518244031,-18.4307490823287,
18.1187322238881));
#180002=CARTESIAN_POINT('Ctrl Pts',(16.6860916186233,-18.4155335575623,
18.1196675317744));
#180003=CARTESIAN_POINT('Ctrl Pts',(16.6876199074586,-18.40973300111,18.1200252863472));
#180004=CARTESIAN_POINT('Ctrl Pts',(16.6908553251563,-18.3976615878375,
18.1207723192251));
#180005=CARTESIAN_POINT('Ctrl Pts',(16.6925667172145,-18.3913919479573,
18.1211617325887));
#180006=CARTESIAN_POINT('Ctrl Pts',(16.6966783608368,-18.376597557661,18.122084030321));
#180007=CARTESIAN_POINT('Ctrl Pts',(16.6991032760193,-18.3680798418789,
18.1226177126458));
#180008=CARTESIAN_POINT('Ctrl Pts',(16.7073169332177,-18.3399013139651,
18.1243922870873));
#180009=CARTESIAN_POINT('Ctrl Pts',(16.7133375992237,-18.3203098304095,
18.1256407199589));
#180010=CARTESIAN_POINT('Ctrl Pts',(16.7277680334014,-18.2756714939648,
18.1285197261513));
#180011=CARTESIAN_POINT('Ctrl Pts',(16.736362351287,-18.2506939993404,18.1301558666793));
#180012=CARTESIAN_POINT('Ctrl Pts',(16.7454193851305,-18.225889720383,18.1318062882837));
#180013=CARTESIAN_POINT('Origin',(18.734,-18.952,0.));
#180014=CARTESIAN_POINT('',(16.7477768045735,-18.2267292102227,19.1554367670381));
#180015=CARTESIAN_POINT('',(16.7454194046824,-18.2258896668369,18.9348454761515));
#180016=CARTESIAN_POINT('',(16.7454193692319,-18.2258897639242,0.));
#180017=CARTESIAN_POINT('',(16.6180378855072,-18.9538841874204,19.1109437209775));
#180018=CARTESIAN_POINT('Ctrl Pts',(16.6180378855072,-18.9538841874204,
19.1109437209775));
#180019=CARTESIAN_POINT('Ctrl Pts',(16.620150035447,-18.7070537460865,19.125774736331));
#180020=CARTESIAN_POINT('Ctrl Pts',(16.6645218904389,-18.4595580919697,
19.1406057516845));
#180021=CARTESIAN_POINT('Ctrl Pts',(16.7477768045735,-18.2267292102227,
19.1554367670381));
#180022=CARTESIAN_POINT('Ctrl Pts',(16.617000874469,-18.9539241884034,19.1115401934235));
#180023=CARTESIAN_POINT('Ctrl Pts',(16.6170652114638,-19.0247079855457,
19.1069028320399));
#180024=CARTESIAN_POINT('Ctrl Pts',(16.6206796002688,-19.0954439547243,
19.1022147600423));
#180025=CARTESIAN_POINT('Ctrl Pts',(16.6387701735723,-19.2736020781264,
19.0903935332217));
#180026=CARTESIAN_POINT('Ctrl Pts',(16.6579618430164,-19.3803535572353,
19.083293761929));
#180027=CARTESIAN_POINT('Ctrl Pts',(16.6882113661698,-19.4965887500812,
19.0758470398698));
#180028=CARTESIAN_POINT('Ctrl Pts',(16.6912765006865,-19.5079755038791,
19.0751207163271));
#180029=CARTESIAN_POINT('Ctrl Pts',(16.6957773496905,-19.5241559699026,
19.0740937428757));
#180030=CARTESIAN_POINT('Ctrl Pts',(16.6971350986209,-19.5289708838746,
19.0737887897188));
#180031=CARTESIAN_POINT('Ctrl Pts',(16.6995074993299,-19.537271254882,19.0732642610191));
#180032=CARTESIAN_POINT('Ctrl Pts',(16.700514067425,-19.5407589828398,19.0730442195897));
#180033=CARTESIAN_POINT('Ctrl Pts',(16.7024856521041,-19.5475250899387,
19.0726180632995));
#180034=CARTESIAN_POINT('Ctrl Pts',(16.703449635275,-19.5508037200546,19.0724118875206));
#180035=CARTESIAN_POINT('Ctrl Pts',(16.7060774471599,-19.5596619284184,
19.0718556859131));
#180036=CARTESIAN_POINT('Ctrl Pts',(16.7077563760127,-19.5652370484889,
19.0715065346915));
#180037=CARTESIAN_POINT('Ctrl Pts',(16.7141061795218,-19.5860116654419,
19.0702086337591));
#180038=CARTESIAN_POINT('Ctrl Pts',(16.7189253847574,-19.6011657467373,
19.0692681703082));
#180039=CARTESIAN_POINT('Ctrl Pts',(16.7615366618779,-19.7301087741614,
19.0613084815078));
#180040=CARTESIAN_POINT('Ctrl Pts',(16.8087671369662,-19.8405667096365,
19.0547667093754));
#180041=CARTESIAN_POINT('Ctrl Pts',(16.8870989036541,-19.987778871475,19.0457035422698));
#180042=CARTESIAN_POINT('Ctrl Pts',(16.9104596223258,-20.0283744664809,
19.043165895331));
#180043=CARTESIAN_POINT('Ctrl Pts',(16.9827337657313,-20.1448544928694,
19.0356933589462));
#180044=CARTESIAN_POINT('Ctrl Pts',(17.0351732310353,-20.2184205215897,
19.0307219844509));
#180045=CARTESIAN_POINT('Ctrl Pts',(17.1225202872451,-20.3257312918419,
19.0228503161085));
#180046=CARTESIAN_POINT('Ctrl Pts',(17.1541589179061,-20.3620021851008,
19.0200699604294));
#180047=CARTESIAN_POINT('Ctrl Pts',(17.1951341025899,-20.4058647071823,
19.0165371051478));
#180048=CARTESIAN_POINT('Ctrl Pts',(17.2033372655788,-20.414498691187,19.0158330775069));
#180049=CARTESIAN_POINT('Ctrl Pts',(17.2158470417529,-20.427444925191,19.0147640720485));
#180050=CARTESIAN_POINT('Ctrl Pts',(17.2201002307986,-20.4318086428753,
19.0144014173986));
#180051=CARTESIAN_POINT('Ctrl Pts',(17.2288317491846,-20.4406900285331,
19.0136584936779));
#180052=CARTESIAN_POINT('Ctrl Pts',(17.2333117158644,-20.4452059927581,
19.0132781544879));
#180053=CARTESIAN_POINT('Ctrl Pts',(17.2430281277644,-20.4549125851703,
19.0124550181459));
#180054=CARTESIAN_POINT('Ctrl Pts',(17.2482714600792,-20.4600961726571,
19.0120119170828));
#180055=CARTESIAN_POINT('Ctrl Pts',(17.2625641643284,-20.4740791374711,
19.0108069560384));
#180056=CARTESIAN_POINT('Ctrl Pts',(17.2716652206148,-20.4828250394491,
19.0100427772123));
#180057=CARTESIAN_POINT('Ctrl Pts',(17.3163414301034,-20.5249958610594,
19.0063059103351));
#180058=CARTESIAN_POINT('Ctrl Pts',(17.3529848115367,-20.5572626678642,
19.003284353189));
#180059=CARTESIAN_POINT('Ctrl Pts',(17.4081689160612,-20.6025669603666,
18.9987923241326));
#180060=CARTESIAN_POINT('Ctrl Pts',(17.4258573728964,-20.6166207270723,
18.9973608634575));
#180061=CARTESIAN_POINT('Ctrl Pts',(17.543364938576,-20.7069527132475,18.9879074241703));
#180062=CARTESIAN_POINT('Ctrl Pts',(17.6495718321833,-20.7744929229256,
18.9796023670809));
#180063=CARTESIAN_POINT('Ctrl Pts',(17.8347824117938,-20.8703259939516,
18.9658293618443));
#180064=CARTESIAN_POINT('Ctrl Pts',(17.9106203525734,-20.9040795704709,
18.9603734206604));
#180065=CARTESIAN_POINT('Ctrl Pts',(18.0226614618614,-20.9462513868634,
18.9527370823941));
#180066=CARTESIAN_POINT('Ctrl Pts',(18.0574095816186,-20.9583067798161,
18.9504257082238));
#180067=CARTESIAN_POINT('Ctrl Pts',(18.0996138954436,-20.9717276251687,
18.9477008309405));
#180068=CARTESIAN_POINT('Ctrl Pts',(18.1067835335827,-20.9739656074384,
18.9472407656497));
#180069=CARTESIAN_POINT('Ctrl Pts',(18.117951200504,-20.9773864463134,18.9465287203413));
#180070=CARTESIAN_POINT('Ctrl Pts',(18.12194098629,-20.978595703316,18.9462752369095));
#180071=CARTESIAN_POINT('Ctrl Pts',(18.1293490443409,-20.980817125907,18.9458062888669));
#180072=CARTESIAN_POINT('Ctrl Pts',(18.1327662697539,-20.9818324340824,
18.9455906469487));
#180073=CARTESIAN_POINT('Ctrl Pts',(18.1405004681003,-20.9841091339077,
18.9451041015624));
#180074=CARTESIAN_POINT('Ctrl Pts',(18.1448188939874,-20.9853654004266,
18.944833498997));
#180075=CARTESIAN_POINT('Ctrl Pts',(18.1559582180083,-20.9885674572621,
18.9441381404782));
#180076=CARTESIAN_POINT('Ctrl Pts',(18.1627850135225,-20.9904927647988,
18.943714548472));
#180077=CARTESIAN_POINT('Ctrl Pts',(18.2043241014246,-21.0019826472857,
18.9411519389684));
#180078=CARTESIAN_POINT('Ctrl Pts',(18.2392683215349,-21.0106952964831,
18.9390589412509));
#180079=CARTESIAN_POINT('Ctrl Pts',(18.289725807202,-21.0219167361447,18.9361041378621));
#180080=CARTESIAN_POINT('Ctrl Pts',(18.3050692561207,-21.0251505713877,
18.9352144701453));
#180081=CARTESIAN_POINT('Ctrl Pts',(18.321324888878,-21.028388463878,18.9342799220557));
#180082=CARTESIAN_POINT('Ctrl Pts',(18.3222023410887,-21.0285626618005,
18.9342295013104));
#180083=CARTESIAN_POINT('Ctrl Pts',(18.3453897870997,-21.0331507202427,
18.9328977330889));
#180084=CARTESIAN_POINT('Ctrl Pts',(18.3677699226102,-21.0372054574691,
18.931628080751));
#180085=CARTESIAN_POINT('Ctrl Pts',(18.5377453444319,-21.0651798041144,
18.9220759273548));
#180086=CARTESIAN_POINT('Ctrl Pts',(18.6874375397328,-21.0737633457977,
18.914148898755));
#180087=CARTESIAN_POINT('Ctrl Pts',(18.895486284219,-21.0636497386645,18.9026000437049));
#180088=CARTESIAN_POINT('Ctrl Pts',(18.9540349283439,-21.0583537951738,
18.8992952396136));
#180089=CARTESIAN_POINT('Ctrl Pts',(19.0479101787959,-21.0459056572862,
18.8938547420006));
#180090=CARTESIAN_POINT('Ctrl Pts',(19.0834080489576,-21.0402754349872,
18.8917646646156));
#180091=CARTESIAN_POINT('Ctrl Pts',(19.1295530010521,-21.0317470157421,
18.8889978805677));
#180092=CARTESIAN_POINT('Ctrl Pts',(19.1403461580014,-21.0296651845554,
18.8883471655341));
#180093=CARTESIAN_POINT('Ctrl Pts',(19.157924918173,-21.026132301998,18.8872813244757));
#180094=CARTESIAN_POINT('Ctrl Pts',(19.1647205497051,-21.0247317599582,
18.8868678158903));
#180095=CARTESIAN_POINT('Ctrl Pts',(19.1778116031673,-21.0219666070966,
18.8860683420336));
#180096=CARTESIAN_POINT('Ctrl Pts',(19.1841079308838,-21.0206066186528,
18.8856825289033));
#180097=CARTESIAN_POINT('Ctrl Pts',(19.1985605790557,-21.017415780284,18.8847939093201));
#180098=CARTESIAN_POINT('Ctrl Pts',(19.2067124191574,-21.0155653231005,
18.8842904779249));
#180099=CARTESIAN_POINT('Ctrl Pts',(19.2284499925962,-21.0104953583301,
18.882942014316));
#180100=CARTESIAN_POINT('Ctrl Pts',(19.2420150201229,-21.0071896895702,
18.8820942229203));
#180101=CARTESIAN_POINT('Ctrl Pts',(19.3520931255273,-20.9792083062091,
18.8751620709404));
#180102=CARTESIAN_POINT('Ctrl Pts',(19.4467735742749,-20.947886147957,18.8688614291534));
#180103=CARTESIAN_POINT('Ctrl Pts',(19.6655329465785,-20.8579603443488,
18.853521703438));
#180104=CARTESIAN_POINT('Ctrl Pts',(19.7868273168242,-20.7937354822206,
18.8443642515389));
#180105=CARTESIAN_POINT('Ctrl Pts',(19.9429078570594,-20.6906048252188,
18.8321474387152));
#180106=CARTESIAN_POINT('Ctrl Pts',(19.9837636513484,-20.6614725593594,
18.8289077999918));
#180107=CARTESIAN_POINT('Ctrl Pts',(20.0447099289925,-20.6146606637014,
18.8240527637777));
#180108=CARTESIAN_POINT('Ctrl Pts',(20.0655634722463,-20.5980072519908,
18.8223873935712));
#180109=CARTESIAN_POINT('Ctrl Pts',(20.091327007782,-20.5766225963108,18.8203304754329));
#180110=CARTESIAN_POINT('Ctrl Pts',(20.0965355111079,-20.572256822348,18.8199146679904));
#180111=CARTESIAN_POINT('Ctrl Pts',(20.104784895633,-20.5652742674967,18.8192562751029));
#180112=CARTESIAN_POINT('Ctrl Pts',(20.1078394666861,-20.5626738380742,
18.8190125248797));
#180113=CARTESIAN_POINT('Ctrl Pts',(20.1136142998931,-20.5577292045004,
18.8185518062909));
#180114=CARTESIAN_POINT('Ctrl Pts',(20.1163359548494,-20.5553867913711,
18.8183347197709));
#180115=CARTESIAN_POINT('Ctrl Pts',(20.1225810586224,-20.5499841746153,
18.8178366811033));
#180116=CARTESIAN_POINT('Ctrl Pts',(20.1261003557378,-20.5469192390823,
18.8175560837868));
#180117=CARTESIAN_POINT('Ctrl Pts',(20.1354925323464,-20.538684875531,18.816807311222));
#180118=CARTESIAN_POINT('Ctrl Pts',(20.1413470019452,-20.5334944302318,
18.8163406550191));
#180119=CARTESIAN_POINT('Ctrl Pts',(20.1844649596188,-20.4948379444219,
18.8129031626051));
#180120=CARTESIAN_POINT('Ctrl Pts',(20.2205622916639,-20.4600885033655,
18.8100220140627));
#180121=CARTESIAN_POINT('Ctrl Pts',(20.2561637673475,-20.4232945610323,
18.8071347119682));
#180122=CARTESIAN_POINT('Ctrl Pts',(20.2569311871159,-20.422500193563,18.8070724512626));
#180123=CARTESIAN_POINT('Ctrl Pts',(20.2676427367322,-20.4113951322806,
18.8062031037568));
#180124=CARTESIAN_POINT('Ctrl Pts',(20.2774827530772,-20.4009841961231,
18.8054006282567));
#180125=CARTESIAN_POINT('Ctrl Pts',(20.3957970167284,-20.2732323812727,
18.7956930308644));
#180126=CARTESIAN_POINT('Ctrl Pts',(20.4907566013449,-20.144071890234,18.7872529699876));
#180127=CARTESIAN_POINT('Ctrl Pts',(20.6095576002548,-19.9369884888591,
18.7740042318909));
#180128=CARTESIAN_POINT('Ctrl Pts',(20.644970273443,-19.8663901298712,18.769538109495));
#180129=CARTESIAN_POINT('Ctrl Pts',(20.6840439820399,-19.7762517870427,
18.7638050068164));
#180130=CARTESIAN_POINT('Ctrl Pts',(20.691487501346,-19.7584150208188,18.7626692709587));
#180131=CARTESIAN_POINT('Ctrl Pts',(20.7019069469471,-19.7324524680005,
18.7610133048494));
#180132=CARTESIAN_POINT('Ctrl Pts',(20.7050790507993,-19.7244060970536,
18.7604996968709));
#180133=CARTESIAN_POINT('Ctrl Pts',(20.7105356330737,-19.7103123879451,
18.7595993130592));
#180134=CARTESIAN_POINT('Ctrl Pts',(20.7128419002785,-19.7042735664588,
18.7592132750103));
#180135=CARTESIAN_POINT('Ctrl Pts',(20.717253308123,-19.6925619001657,18.7584640825683));
#180136=CARTESIAN_POINT('Ctrl Pts',(20.7193618587849,-19.6868904004394,
18.7581010469064));
#180137=CARTESIAN_POINT('Ctrl Pts',(20.7243240304092,-19.6733661089447,
18.7572347651345));
#180138=CARTESIAN_POINT('Ctrl Pts',(20.7271555172221,-19.6655053540056,
18.7567307863553));
#180139=CARTESIAN_POINT('Ctrl Pts',(20.7370939714386,-19.6373934334635,
18.7549266507367));
#180140=CARTESIAN_POINT('Ctrl Pts',(20.7439392410429,-19.6170517356877,
18.7536178675147));
#180141=CARTESIAN_POINT('Ctrl Pts',(20.8087912100549,-19.4141813327006,
18.7405283510565));
#180142=CARTESIAN_POINT('Ctrl Pts',(20.84207179726,-19.2247143729517,18.7278883131169));
#180143=CARTESIAN_POINT('Ctrl Pts',(20.8523695349017,-18.957134575205,18.7102207957596));
#180144=CARTESIAN_POINT('Ctrl Pts',(20.8511775341112,-18.8807488283608,
18.7052146034663));
#180145=CARTESIAN_POINT('Ctrl Pts',(20.8434255922919,-18.7696911120313,
18.6981244729446));
#180146=CARTESIAN_POINT('Ctrl Pts',(20.8401247623566,-18.7348556347325,
18.6959281023601));
#180147=CARTESIAN_POINT('Ctrl Pts',(20.8350811045628,-18.6927665563776,
18.6933205148));
#180148=CARTESIAN_POINT('Ctrl Pts',(20.8341618770439,-18.6854219060445,
18.6928671951307));
#180149=CARTESIAN_POINT('Ctrl Pts',(20.8326677828748,-18.6739717280811,
18.692163308659));
#180150=CARTESIAN_POINT('Ctrl Pts',(20.8321193573371,-18.6698628951892,
18.6919112923699));
#180151=CARTESIAN_POINT('Ctrl Pts',(20.8310765119621,-18.6622210688013,
18.691443672769));
#180152=CARTESIAN_POINT('Ctrl Pts',(20.8305852355322,-18.6586877493163,
18.6912279008464));
#180153=CARTESIAN_POINT('Ctrl Pts',(20.8294498587385,-18.6506705984575,
18.6907392946298));
#180154=CARTESIAN_POINT('Ctrl Pts',(20.8288002986951,-18.6461875931485,
18.690466772157));
#180155=CARTESIAN_POINT('Ctrl Pts',(20.8270811542106,-18.634585272112,18.6897631854897));
#180156=CARTESIAN_POINT('Ctrl Pts',(20.8259896246901,-18.6274691984896,
18.6893333318601));
#180157=CARTESIAN_POINT('Ctrl Pts',(20.8189514966166,-18.5830966976193,
18.6866626748909));
#180158=CARTESIAN_POINT('Ctrl Pts',(20.8120457445476,-18.5459967153876,
18.6844724648767));
#180159=CARTESIAN_POINT('Ctrl Pts',(20.7686152836847,-18.3429997244225,
18.6726271440897));
#180160=CARTESIAN_POINT('Ctrl Pts',(20.7132153880081,-18.1817670269906,
18.6636884066837));
#180161=CARTESIAN_POINT('Ctrl Pts',(20.5977361780559,-17.9434419168421,
18.6491175835415));
#180162=CARTESIAN_POINT('Ctrl Pts',(20.5506434548851,-17.8608971327872,
18.6437932139985));
#180163=CARTESIAN_POINT('Ctrl Pts',(20.4863803687323,-17.7640154423997,
18.6370231707435));
#180164=CARTESIAN_POINT('Ctrl Pts',(20.4743182342881,-17.7464143911656,
18.6357711300839));
#180165=CARTESIAN_POINT('Ctrl Pts',(20.4567927594812,-17.7216524400462,
18.6339766030276));
#180166=CARTESIAN_POINT('Ctrl Pts',(20.4515463460132,-17.7143390787895,
18.6334424111073));
#180167=CARTESIAN_POINT('Ctrl Pts',(20.4424165214023,-17.7017821943033,
18.6325178606856));
#180168=CARTESIAN_POINT('Ctrl Pts',(20.4385551833193,-17.6965227211013,
18.6321283602091));
#180169=CARTESIAN_POINT('Ctrl Pts',(20.4311162969374,-17.6864878993819,
18.6313808487706));
#180170=CARTESIAN_POINT('Ctrl Pts',(20.427542747514,-17.6817096539171,18.6310229963873));
#180171=CARTESIAN_POINT('Ctrl Pts',(20.4181998355861,-17.6693266073927,
18.6300905803239));
#180172=CARTESIAN_POINT('Ctrl Pts',(20.4123992004189,-17.6617456693907,
18.6295147893487));
#180173=CARTESIAN_POINT('Ctrl Pts',(20.3924552839219,-17.636042741397,18.6275454130094));
#180174=CARTESIAN_POINT('Ctrl Pts',(20.3780685804972,-17.6181124963164,
18.6261421830574));
#180175=CARTESIAN_POINT('Ctrl Pts',(20.2512922901167,-17.4652776528622,
18.6139197872578));
#180176=CARTESIAN_POINT('Ctrl Pts',(20.122833607584,-17.3446304201945,18.602396066731));
#180177=CARTESIAN_POINT('Ctrl Pts',(19.9107367932032,-17.1900298770749,
18.5850549848006));
#180178=CARTESIAN_POINT('Ctrl Pts',(19.8373844545476,-17.1431902102999,
18.5793250580783));
#180179=CARTESIAN_POINT('Ctrl Pts',(19.728299771966,-17.0826455043845,18.571359781479));
#180180=CARTESIAN_POINT('Ctrl Pts',(19.6947562758084,-17.0651862691705,
18.5689817325433));
#180181=CARTESIAN_POINT('Ctrl Pts',(19.6539540959718,-17.0453194348311,
18.5661891346508));
#180182=CARTESIAN_POINT('Ctrl Pts',(19.6471294859879,-17.0420416595946,
18.5657253429366));
#180183=CARTESIAN_POINT('Ctrl Pts',(19.6365078851409,-17.0370101810516,
18.5650087938176));
#180184=CARTESIAN_POINT('Ctrl Pts',(19.6327231138948,-17.0352310377443,
18.564754502849));
#180185=CARTESIAN_POINT('Ctrl Pts',(19.6257034045994,-17.0319565790059,
18.5642848126053));
#180186=CARTESIAN_POINT('Ctrl Pts',(19.6224699909983,-17.0304582295274,
18.5640692312618));
#180187=CARTESIAN_POINT('Ctrl Pts',(19.6151630084797,-17.0270945932702,
18.5635837702082));
#180188=CARTESIAN_POINT('Ctrl Pts',(19.6110873043842,-17.0252340739708,
18.5633141856012));
#180189=CARTESIAN_POINT('Ctrl Pts',(19.5990740855356,-17.0197961735086,
18.5625230093283));
#180190=CARTESIAN_POINT('Ctrl Pts',(19.5911202624566,-17.0162547527759,
18.5620035739807));
#180191=CARTESIAN_POINT('Ctrl Pts',(19.5344972672616,-16.9914609291305,
18.5583352841853));
#180192=CARTESIAN_POINT('Ctrl Pts',(19.4850610859561,-16.9719955616644,
18.5552869015237));
#180193=CARTESIAN_POINT('Ctrl Pts',(19.4326900253195,-16.9536189205482,
18.552164966228));
#180194=CARTESIAN_POINT('Ctrl Pts',(19.4304378215955,-16.9528329107057,
18.5520309130727));
#180195=CARTESIAN_POINT('Ctrl Pts',(19.2889259380069,-16.9037140023828,
18.5436205846945));
#180196=CARTESIAN_POINT('Ctrl Pts',(19.144993167015,-16.870051761806,18.535804091456));
#180197=CARTESIAN_POINT('Ctrl Pts',(18.9017579375211,-16.8393954862422,
18.5223328984335));
#180198=CARTESIAN_POINT('Ctrl Pts',(18.804073857189,-16.8339048737711,18.5168602449389));
#180199=CARTESIAN_POINT('Ctrl Pts',(18.6847002714384,-16.8354631937374,
18.5099105147111));
#180200=CARTESIAN_POINT('Ctrl Pts',(18.6630400526057,-16.8360786521938,
18.5086393220794));
#180201=CARTESIAN_POINT('Ctrl Pts',(18.6323460040724,-16.8374226232391,
18.5068220849068));
#180202=CARTESIAN_POINT('Ctrl Pts',(18.6233010830058,-16.8378768335093,
18.5062846281345));
#180203=CARTESIAN_POINT('Ctrl Pts',(18.6077349798491,-16.8387586862463,
18.5053562071911));
#180204=CARTESIAN_POINT('Ctrl Pts',(18.6012123030525,-16.8391585171784,
18.5049661204298));
#180205=CARTESIAN_POINT('Ctrl Pts',(18.5887491576818,-16.8399804310905,
18.5042187190399));
#180206=CARTESIAN_POINT('Ctrl Pts',(18.5828084053839,-16.8403973936268,
18.5038615689527));
#180207=CARTESIAN_POINT('Ctrl Pts',(18.5674130771166,-16.8415432444234,
18.502933678824));
#180208=CARTESIAN_POINT('Ctrl Pts',(18.5579615745834,-16.8423105943681,
18.5023617350231));
#180209=CARTESIAN_POINT('Ctrl Pts',(18.5259970074067,-16.8451220329862,
18.5004195123274));
#180210=CARTESIAN_POINT('Ctrl Pts',(18.5035122386515,-16.8474631524947,
18.4990399459163));
#180211=CARTESIAN_POINT('Ctrl Pts',(18.3020366076918,-16.8717082602263,
18.4865540254973));
#180212=CARTESIAN_POINT('Ctrl Pts',(18.1265215968773,-16.9160356784934,
18.4746992235394));
#180213=CARTESIAN_POINT('Ctrl Pts',(17.8809234710159,-17.0126828452792,
18.4572661424599));
#180214=CARTESIAN_POINT('Ctrl Pts',(17.8049397264581,-17.0479150690734,
18.4517595148268));
#180215=CARTESIAN_POINT('Ctrl Pts',(17.6986814552425,-17.1050644421313,
18.4440621133919));
#180216=CARTESIAN_POINT('Ctrl Pts',(17.6665877604628,-17.1234248881538,
18.441738217114));
#180217=CARTESIAN_POINT('Ctrl Pts',(17.6285601949496,-17.146522661701,18.4390006060156));
#180218=CARTESIAN_POINT('Ctrl Pts',(17.6221518817284,-17.1504619494723,
18.4385398308868));
#180219=CARTESIAN_POINT('Ctrl Pts',(17.612222568142,-17.1566388122636,18.4378269274789));
#180220=CARTESIAN_POINT('Ctrl Pts',(17.6086870295047,-17.1588527332691,
18.437573290062));
#180221=CARTESIAN_POINT('Ctrl Pts',(17.6021424077684,-17.1629778934257,
18.4371042010841));
#180222=CARTESIAN_POINT('Ctrl Pts',(17.5991316352445,-17.1648862649878,
18.4368885713057));
#180223=CARTESIAN_POINT('Ctrl Pts',(17.5923359161326,-17.1692178157897,
18.4364022353642));
#180224=CARTESIAN_POINT('Ctrl Pts',(17.5885538671497,-17.1716454414009,
18.4361318289867));
#180225=CARTESIAN_POINT('Ctrl Pts',(17.5774136063864,-17.1788463573483,
18.435335998597));
#180226=CARTESIAN_POINT('Ctrl Pts',(17.5700771912056,-17.1836534198499,
18.4348127690381));
#180227=CARTESIAN_POINT('Ctrl Pts',(17.5172408467851,-17.2187448206347,
18.4310491594108));
#180228=CARTESIAN_POINT('Ctrl Pts',(17.4728948475057,-17.2507383396572,
18.4279152641341));
#180229=CARTESIAN_POINT('Ctrl Pts',(17.2972522732232,-17.3881030042149,
18.41538893972));
#180230=CARTESIAN_POINT('Ctrl Pts',(17.1775038974791,-17.5072352240484,
18.406530471036));
#180231=CARTESIAN_POINT('Ctrl Pts',(17.0365796077152,-17.6855378391791,
18.3939311523265));
#180232=CARTESIAN_POINT('Ctrl Pts',(17.0019842259434,-17.733278133765,18.3906172203878));
#180233=CARTESIAN_POINT('Ctrl Pts',(16.9495311335903,-17.81241379327,18.3851630515493));
#180234=CARTESIAN_POINT('Ctrl Pts',(16.9304053205674,-17.8429319841393,
18.3830687313743));
#180235=CARTESIAN_POINT('Ctrl Pts',(16.9064660573374,-17.8833888946915,
18.3802971110623));
#180236=CARTESIAN_POINT('Ctrl Pts',(16.9009381459161,-17.8928993257645,
18.3796459180194));
#180237=CARTESIAN_POINT('Ctrl Pts',(16.8920438930034,-17.9084795798079,
18.3785794903944));
#180238=CARTESIAN_POINT('Ctrl Pts',(16.8886327949576,-17.914523713885,18.378165876683));
#180239=CARTESIAN_POINT('Ctrl Pts',(16.8821134573732,-17.9262092227942,
18.3773663372498));
#180240=CARTESIAN_POINT('Ctrl Pts',(16.8790011178966,-17.9318482312244,
18.3769805644079));
#180241=CARTESIAN_POINT('Ctrl Pts',(16.8719106741465,-17.9448345960143,
18.3760922344689));
#180242=CARTESIAN_POINT('Ctrl Pts',(16.8679502554473,-17.9521914402386,
18.3755890537669));
#180243=CARTESIAN_POINT('Ctrl Pts',(16.8574949048652,-17.9718917552561,
18.3742416978715));
#180244=CARTESIAN_POINT('Ctrl Pts',(16.8510783203701,-17.9842761358493,
18.3733947706254));
#180245=CARTESIAN_POINT('Ctrl Pts',(16.807171029365,-18.0711099105015,18.367456078307));
#180246=CARTESIAN_POINT('Ctrl Pts',(16.7739942120167,-18.147632526116,18.362216055964));
#180247=CARTESIAN_POINT('Ctrl Pts',(16.7454193588142,-18.2258897924551,
18.356854558525));
#180248=CARTESIAN_POINT('',(16.6170000449379,-18.9515638040726,18.8870727812038));
#180249=CARTESIAN_POINT('Ctrl Pts',(16.7454193851305,-18.225889720383,18.1318062882837));
#180250=CARTESIAN_POINT('Ctrl Pts',(16.7665449585877,-18.1680336246436,
18.1356559043328));
#180251=CARTESIAN_POINT('Ctrl Pts',(16.7901879235971,-18.11111997658,18.1395843126614));
#180252=CARTESIAN_POINT('Ctrl Pts',(16.8711047733789,-17.938065988932,18.1519520858756));
#180253=CARTESIAN_POINT('Ctrl Pts',(16.9365617134726,-17.8260991331353,
18.1605860013658));
#180254=CARTESIAN_POINT('Ctrl Pts',(17.027571406272,-17.6987946938612,18.1708505942142));
#180255=CARTESIAN_POINT('Ctrl Pts',(17.0437391931054,-17.6770723296644,
18.1726183489123));
#180256=CARTESIAN_POINT('Ctrl Pts',(17.0954975693988,-17.6102477688841,
18.1780951904285));
#180257=CARTESIAN_POINT('Ctrl Pts',(17.1325132009441,-17.566276161235,18.1817560508463));
#180258=CARTESIAN_POINT('Ctrl Pts',(17.1772632991259,-17.5173088715787,
18.1858493168984));
#180259=CARTESIAN_POINT('Ctrl Pts',(17.1832926097607,-17.5107941208812,
18.1863942385789));
#180260=CARTESIAN_POINT('Ctrl Pts',(17.1924515195223,-17.5010218186135,
18.1872118886485));
#180261=CARTESIAN_POINT('Ctrl Pts',(17.1955507732445,-17.4977361387655,
18.187486845595));
#180262=CARTESIAN_POINT('Ctrl Pts',(17.2011159192302,-17.4918739392213,
18.1879774508873));
#180263=CARTESIAN_POINT('Ctrl Pts',(17.203577819605,-17.4892937175194,18.1881933989095));
#180264=CARTESIAN_POINT('Ctrl Pts',(17.2089219344602,-17.4837210226793,
18.1886598143095));
#180265=CARTESIAN_POINT('Ctrl Pts',(17.21180643224,-17.4807308185842,18.188910099766));
#180266=CARTESIAN_POINT('Ctrl Pts',(17.219884348895,-17.4724060613665,18.1896070073417));
#180267=CARTESIAN_POINT('Ctrl Pts',(17.2250971918987,-17.4670903234193,
18.1900521420559));
#180268=CARTESIAN_POINT('Ctrl Pts',(17.2554545728113,-17.4364586612858,
18.1926187445845));
#180269=CARTESIAN_POINT('Ctrl Pts',(17.2812094973664,-17.4117525444168,
18.1946949947162));
#180270=CARTESIAN_POINT('Ctrl Pts',(17.3658491794521,-17.3345726732887,
18.2012494691061));
#180271=CARTESIAN_POINT('Ctrl Pts',(17.4270482459534,-17.2847307130793,
18.205590639856));
#180272=CARTESIAN_POINT('Ctrl Pts',(17.5646209109373,-17.184929349456,18.2148598574735));
#180273=CARTESIAN_POINT('Ctrl Pts',(17.6417259456608,-17.1362567900831,
18.2197668998467));
#180274=CARTESIAN_POINT('Ctrl Pts',(17.8150507045617,-17.0418920553965,
18.2306130202343));
#180275=CARTESIAN_POINT('Ctrl Pts',(17.9120567877858,-16.9981869926977,
18.2365759856562));
#180276=CARTESIAN_POINT('Ctrl Pts',(18.0251851384886,-16.9571392406406,
18.2436279186341));
#180277=CARTESIAN_POINT('Ctrl Pts',(18.0384920110797,-16.952460908076,18.2444586991437));
#180278=CARTESIAN_POINT('Ctrl Pts',(18.0597973654308,-16.9452089333397,
18.2457913137286));
#180279=CARTESIAN_POINT('Ctrl Pts',(18.0677662793405,-16.9425492780265,
18.2462903024008));
#180280=CARTESIAN_POINT('Ctrl Pts',(18.0818792474372,-16.9379322000762,
18.2471750621814));
#180281=CARTESIAN_POINT('Ctrl Pts',(18.0880168436865,-16.9359552735735,
18.2475601848501));
#180282=CARTESIAN_POINT('Ctrl Pts',(18.1007601237863,-16.9319148157044,
18.2483605652292));
#180283=CARTESIAN_POINT('Ctrl Pts',(18.1073670781434,-16.9298555758517,
18.2487759586172));
#180284=CARTESIAN_POINT('Ctrl Pts',(18.1244158085745,-16.9246334452194,
18.2498489949708));
#180285=CARTESIAN_POINT('Ctrl Pts',(18.1348720557028,-16.9215188419338,
18.2505082093358));
#180286=CARTESIAN_POINT('Ctrl Pts',(18.1791643074843,-16.9086974173438,
18.2533055816813));
#180287=CARTESIAN_POINT('Ctrl Pts',(18.2132139978124,-16.8997549375528,
18.2554683985051));
#180288=CARTESIAN_POINT('Ctrl Pts',(18.3030415105969,-16.8785429190307,
18.2612097537341));
#180289=CARTESIAN_POINT('Ctrl Pts',(18.3591176582475,-16.867674735274,18.2648299754842));
#180290=CARTESIAN_POINT('Ctrl Pts',(18.565926584198,-16.8362085130913,18.2782974231191));
#180291=CARTESIAN_POINT('Ctrl Pts',(18.7183156812933,-16.8296028862274,
18.2884830967201));
#180292=CARTESIAN_POINT('Ctrl Pts',(18.8925923659588,-16.8408281484325,
18.2998897592546));
#180293=CARTESIAN_POINT('Ctrl Pts',(18.9150854607903,-16.8426384302645,
18.3013563651973));
#180294=CARTESIAN_POINT('Ctrl Pts',(18.9886367327381,-16.8497431724784,
18.3061256908033));
#180295=CARTESIAN_POINT('Ctrl Pts',(19.0395359702751,-16.8565352923416,
18.3093846572935));
#180296=CARTESIAN_POINT('Ctrl Pts',(19.0979044103317,-16.8664965623328,
18.313036717202));
#180297=CARTESIAN_POINT('Ctrl Pts',(19.1056594076537,-16.8678646163246,
18.3135201862963));
#180298=CARTESIAN_POINT('Ctrl Pts',(19.1180124860542,-16.8701149581386,
18.3142873174329));
#180299=CARTESIAN_POINT('Ctrl Pts',(19.1226154997471,-16.8709692670943,
18.3145725017371));
#180300=CARTESIAN_POINT('Ctrl Pts',(19.1307460827797,-16.8725062022651,
18.315075018466));
#180301=CARTESIAN_POINT('Ctrl Pts',(19.1342747962258,-16.8731825483529,
18.3152927044161));
#180302=CARTESIAN_POINT('Ctrl Pts',(19.1417318290641,-16.8746315243847,
18.3157518485651));
#180303=CARTESIAN_POINT('Ctrl Pts',(19.1456596764027,-16.8754063133708,
18.315993182057));
#180304=CARTESIAN_POINT('Ctrl Pts',(19.1562137929178,-16.8775192913628,
18.3166403252247));
#180305=CARTESIAN_POINT('Ctrl Pts',(19.1628359541204,-16.8788780969971,
18.3170449741432));
#180306=CARTESIAN_POINT('Ctrl Pts',(19.1951516894006,-16.8856704536718,
18.3190132925926));
#180307=CARTESIAN_POINT('Ctrl Pts',(19.2207503853085,-16.8915503209158,
18.320552870753));
#180308=CARTESIAN_POINT('Ctrl Pts',(19.2937734347693,-16.9097602473839,
18.3249054532179));
#180309=CARTESIAN_POINT('Ctrl Pts',(19.340889889245,-16.9232627574063,18.3276661414446));
#180310=CARTESIAN_POINT('Ctrl Pts',(19.4793748859793,-16.9682067386742,
18.3357497549167));
#180311=CARTESIAN_POINT('Ctrl Pts',(19.5691064443162,-17.004278741696,18.340951245465));
#180312=CARTESIAN_POINT('Ctrl Pts',(19.7830127616348,-17.1077791966131,
18.3538818185892));
#180313=CARTESIAN_POINT('Ctrl Pts',(19.9034880253291,-17.1817264693793,
18.3616606999173));
#180314=CARTESIAN_POINT('Ctrl Pts',(20.0270784958069,-17.2757419618227,
18.3707579136162));
#180315=CARTESIAN_POINT('Ctrl Pts',(20.0383582927647,-17.2845041421101,
18.3715990264613));
#180316=CARTESIAN_POINT('Ctrl Pts',(20.0561708817946,-17.2986323433455,
18.3729450921797));
#180317=CARTESIAN_POINT('Ctrl Pts',(20.0627618103235,-17.3039246082167,
18.3734471074083));
#180318=CARTESIAN_POINT('Ctrl Pts',(20.0743308976924,-17.3133286567577,
18.3743353854216));
#180319=CARTESIAN_POINT('Ctrl Pts',(20.0793222992395,-17.317424031678,18.3747209828259));
#180320=CARTESIAN_POINT('Ctrl Pts',(20.0896082613464,-17.3259425478382,
18.3755205301221));
#180321=CARTESIAN_POINT('Ctrl Pts',(20.0949000849509,-17.3303688603787,
18.3759346067145));
#180322=CARTESIAN_POINT('Ctrl Pts',(20.1084298887783,-17.3417986482614,
18.3770003927451));
#180323=CARTESIAN_POINT('Ctrl Pts',(20.1166359453447,-17.348839450287,18.3776536332136));
#180324=CARTESIAN_POINT('Ctrl Pts',(20.1506772188183,-17.3785026589924,
18.3803924522826));
#180325=CARTESIAN_POINT('Ctrl Pts',(20.1760128201895,-17.4016880849536,
18.3825014210998));
#180326=CARTESIAN_POINT('Ctrl Pts',(20.2405625543297,-17.4637112869645,
18.388065843649));
#180327=CARTESIAN_POINT('Ctrl Pts',(20.2788398281181,-17.5034824458097,
18.391559854416));
#180328=CARTESIAN_POINT('Ctrl Pts',(20.3882817034996,-17.626472804715,18.4021426913351));
#180329=CARTESIAN_POINT('Ctrl Pts',(20.4545893180642,-17.7137596217042,
18.4093798637376));
#180330=CARTESIAN_POINT('Ctrl Pts',(20.5426716995883,-17.8505327819045,
18.4201260338893));
#180331=CARTESIAN_POINT('Ctrl Pts',(20.5697993579742,-17.8963654025274,
18.4236350106244));
#180332=CARTESIAN_POINT('Ctrl Pts',(20.6009705582955,-17.9538727284765,
18.4278922748696));
#180333=CARTESIAN_POINT('Ctrl Pts',(20.6066778448426,-17.9646222539345,
18.4286819727962));
#180334=CARTESIAN_POINT('Ctrl Pts',(20.6371280927676,-18.023188367161,18.4329494639269));
#180335=CARTESIAN_POINT('Ctrl Pts',(20.6601351117941,-18.0718908135102,
18.4363729718975));
#180336=CARTESIAN_POINT('Ctrl Pts',(20.6846901874173,-18.1294593325879,
18.4402339214409));
#180337=CARTESIAN_POINT('Ctrl Pts',(20.6880687963992,-18.1375182618265,
18.4407702610931));
#180338=CARTESIAN_POINT('Ctrl Pts',(20.693106683554,-18.149746837719,18.4415775823957));
#180339=CARTESIAN_POINT('Ctrl Pts',(20.6948027156616,-18.1539011057223,
18.441850711488));
#180340=CARTESIAN_POINT('Ctrl Pts',(20.6978222163122,-18.1613648085102,
18.4423393539879));
#180341=CARTESIAN_POINT('Ctrl Pts',(20.6991505413169,-18.1646722068587,
18.442555156883));
#180342=CARTESIAN_POINT('Ctrl Pts',(20.7020173757888,-18.1718627979906,
18.4430227446317));
#180343=CARTESIAN_POINT('Ctrl Pts',(20.7035527430864,-18.1757471814812,
18.4432743395604));
#180344=CARTESIAN_POINT('Ctrl Pts',(20.7078298736014,-18.1866624407219,
18.4439786014567));
#180345=CARTESIAN_POINT('Ctrl Pts',(20.7105455848225,-18.193703550998,18.4444297297222));
#180346=CARTESIAN_POINT('Ctrl Pts',(20.7264897761969,-18.2357102130028,
18.4471031370647));
#180347=CARTESIAN_POINT('Ctrl Pts',(20.7388287216077,-18.2710089936091,
18.4492756847059));
#180348=CARTESIAN_POINT('Ctrl Pts',(20.7762282916268,-18.3878484388335,
18.4562831207746));
#180349=CARTESIAN_POINT('Ctrl Pts',(20.7972989726569,-18.4705822758739,
18.4609582264682));
#180350=CARTESIAN_POINT('Ctrl Pts',(20.8467445313053,-18.729145644127,18.47528765741));
#180351=CARTESIAN_POINT('Ctrl Pts',(20.8579961072368,-18.907418831783,18.4848422731155));
#180352=CARTESIAN_POINT('Ctrl Pts',(20.8453858381803,-19.1077524797247,
18.4965085929344));
#180353=CARTESIAN_POINT('Ctrl Pts',(20.843585710898,-19.1304854658528,18.4978447068983));
#180354=CARTESIAN_POINT('Ctrl Pts',(20.8405145062713,-19.1626565346894,
18.499754658173));
#180355=CARTESIAN_POINT('Ctrl Pts',(20.8395464017098,-19.1721224352315,
18.500318984759));
#180356=CARTESIAN_POINT('Ctrl Pts',(20.8378680474266,-19.1875074856109,
18.5012401334012));
#180357=CARTESIAN_POINT('Ctrl Pts',(20.8371965449799,-19.1934307951084,
18.5015957311858));
#180358=CARTESIAN_POINT('Ctrl Pts',(20.8357371187209,-19.2058360087118,
18.5023424896483));
#180359=CARTESIAN_POINT('Ctrl Pts',(20.8349442072579,-19.2123172526645,
18.5027338041273));
#180360=CARTESIAN_POINT('Ctrl Pts',(20.8329836830202,-19.2277498652794,
18.5036683860005));
#180361=CARTESIAN_POINT('Ctrl Pts',(20.8317887815874,-19.2366975828618,
18.5042125102485));
#180362=CARTESIAN_POINT('Ctrl Pts',(20.8275553119192,-19.2669240739115,
18.5060584263487));
#180363=CARTESIAN_POINT('Ctrl Pts',(20.8242499870448,-19.2881635830734,
18.5073686159888));
#180364=CARTESIAN_POINT('Ctrl Pts',(20.7903285634653,-19.4862368617905,
18.5197137797789));
#180365=CARTESIAN_POINT('Ctrl Pts',(20.7376707225816,-19.6585228129816,
18.5314928065808));
#180366=CARTESIAN_POINT('Ctrl Pts',(20.6144200890412,-19.9319123596205,
18.5513053303523));
#180367=CARTESIAN_POINT('Ctrl Pts',(20.5556040619444,-20.0373447850727,
18.5592365127184));
#180368=CARTESIAN_POINT('Ctrl Pts',(20.4828132041204,-20.1450765017447,
18.5672667690492));
#180369=CARTESIAN_POINT('Ctrl Pts',(20.4774442085239,-20.1529085982732,
18.5678500457554));
#180370=CARTESIAN_POINT('Ctrl Pts',(20.4694073228555,-20.1644650118824,
18.5687095838543));
#180371=CARTESIAN_POINT('Ctrl Pts',(20.4667798352359,-20.168217096069,18.5689884815663));
#180372=CARTESIAN_POINT('Ctrl Pts',(20.4620818638478,-20.1748797280888,
18.5694833719108));
#180373=CARTESIAN_POINT('Ctrl Pts',(20.4600161760259,-20.1777935871438,
18.5696996861153));
#180374=CARTESIAN_POINT('Ctrl Pts',(20.4555575211057,-20.1840493477613,
18.570163817757));
#180375=CARTESIAN_POINT('Ctrl Pts',(20.4531622003528,-20.1873895026806,
18.5704114696076));
#180376=CARTESIAN_POINT('Ctrl Pts',(20.4465195932349,-20.1965955528215,
18.5710936534573));
#180377=CARTESIAN_POINT('Ctrl Pts',(20.4422518654122,-20.2024467262059,
18.5715267983814));
#180378=CARTESIAN_POINT('Ctrl Pts',(20.418642073164,-20.2344699468653,18.5738956669682));
#180379=CARTESIAN_POINT('Ctrl Pts',(20.3987273804613,-20.2602167596331,
18.5757939322477));
#180380=CARTESIAN_POINT('Ctrl Pts',(20.2757569702404,-20.4118416322731,
18.587002813859));
#180381=CARTESIAN_POINT('Ctrl Pts',(20.1590564167636,-20.525968930747,18.5956012035725));
#180382=CARTESIAN_POINT('Ctrl Pts',(19.9380286479564,-20.6971828982146,
18.610907039946));
#180383=CARTESIAN_POINT('Ctrl Pts',(19.8398780886808,-20.7609711771762,
18.6174315818076));
#180384=CARTESIAN_POINT('Ctrl Pts',(19.7244080862297,-20.8230917722246,
18.6251132076641));
#180385=CARTESIAN_POINT('Ctrl Pts',(19.7117745495097,-20.8297245572347,
18.6259534874781));
#180386=CARTESIAN_POINT('Ctrl Pts',(19.691555525141,-20.8400804523968,18.6272984691493));
#180387=CARTESIAN_POINT('Ctrl Pts',(19.6840129931034,-20.8438868063997,
18.6278002408497));
#180388=CARTESIAN_POINT('Ctrl Pts',(19.6706671524227,-20.85052187853,18.6286882352782));
#180389=CARTESIAN_POINT('Ctrl Pts',(19.6648732775618,-20.8533694058181,
18.6290737939911));
#180390=CARTESIAN_POINT('Ctrl Pts',(19.6528595246483,-20.8592057553701,
18.6298734058691));
#180391=CARTESIAN_POINT('Ctrl Pts',(19.6466378831849,-20.8621907527196,
18.630287586449));
#180392=CARTESIAN_POINT('Ctrl Pts',(19.6306234291891,-20.8697780125836,
18.6313539454941));
#180393=CARTESIAN_POINT('Ctrl Pts',(19.6208098143493,-20.874335669358,18.6320076581667));
#180394=CARTESIAN_POINT('Ctrl Pts',(19.5796456580451,-20.8930709090781,
18.6347510614082));
#180395=CARTESIAN_POINT('Ctrl Pts',(19.5479882159574,-20.9065577042136,
18.6368642402159));
#180396=CARTESIAN_POINT('Ctrl Pts',(19.4646003260422,-20.9397056260535,
18.6424424270416));
#180397=CARTESIAN_POINT('Ctrl Pts',(19.4124053896095,-20.9581195849772,
18.6459462303035));
#180398=CARTESIAN_POINT('Ctrl Pts',(19.2548630933418,-21.0068476894645,
18.6565478666252));
#180399=CARTESIAN_POINT('Ctrl Pts',(19.1478245025441,-21.0310486308391,
18.6637939813457));
#180400=CARTESIAN_POINT('Ctrl Pts',(18.9796595985377,-21.0555649677902,
18.6750194532467));
#180401=CARTESIAN_POINT('Ctrl Pts',(18.9195680272076,-21.0617154450963,
18.6789972395196));
#180402=CARTESIAN_POINT('Ctrl Pts',(18.8011480408859,-21.0687363924581,
18.6866874927192));
#180403=CARTESIAN_POINT('Ctrl Pts',(18.7428788892897,-21.0697828704326,
18.6904010721149));
#180404=CARTESIAN_POINT('Ctrl Pts',(18.6757329433062,-21.068216730707,18.694545712184));
#180405=CARTESIAN_POINT('Ctrl Pts',(18.6668314596741,-21.0679529046746,
18.6950924210869));
#180406=CARTESIAN_POINT('Ctrl Pts',(18.6534118171392,-21.0674703970495,
18.6959122202519));
#180407=CARTESIAN_POINT('Ctrl Pts',(18.6488923895553,-21.0672933960876,
18.6961875561341));
#180408=CARTESIAN_POINT('Ctrl Pts',(18.6408099464247,-21.0669509062252,
18.6966785703841));
#180409=CARTESIAN_POINT('Ctrl Pts',(18.6372467617224,-21.0667908958869,
18.6968945505375));
#180410=CARTESIAN_POINT('Ctrl Pts',(18.6295383728568,-21.0664252156676,
18.6973607322357));
#180411=CARTESIAN_POINT('Ctrl Pts',(18.6253933770102,-21.0662163622294,
18.697610753483));
#180412=CARTESIAN_POINT('Ctrl Pts',(18.6138349381355,-21.0655998869962,
18.6983061800108));
#180413=CARTESIAN_POINT('Ctrl Pts',(18.6064229018036,-21.065165448356,18.698750108121));
#180414=CARTESIAN_POINT('Ctrl Pts',(18.5637356133649,-21.0624380175422,
18.7012958839528));
#180415=CARTESIAN_POINT('Ctrl Pts',(18.5285176721152,-21.0593006265802,
18.7033533677342));
#180416=CARTESIAN_POINT('Ctrl Pts',(18.4162446755172,-21.04645702772,18.7098219918581));
#180417=CARTESIAN_POINT('Ctrl Pts',(18.3396344792758,-21.0333928980314,
18.7141001833032));
#180418=CARTESIAN_POINT('Ctrl Pts',(18.0791980983001,-20.9740810181825,
18.7286736677836));
#180419=CARTESIAN_POINT('Ctrl Pts',(17.900988834018,-20.9074191197759,18.7387863176717));
#180420=CARTESIAN_POINT('Ctrl Pts',(17.7149090153111,-20.8076974426352,
18.7510701684566));
#180421=CARTESIAN_POINT('Ctrl Pts',(17.695950837639,-20.7971594291215,18.7523419856698));
#180422=CARTESIAN_POINT('Ctrl Pts',(17.6698873657972,-20.7821430870851,
18.7541202974416));
#180423=CARTESIAN_POINT('Ctrl Pts',(17.6626413651777,-20.7779107563037,
18.7546179383417));
#180424=CARTESIAN_POINT('Ctrl Pts',(17.6502060398234,-20.7705478764707,
18.7554776666709));
#180425=CARTESIAN_POINT('Ctrl Pts',(17.645004606854,-20.7674378974956,18.7558390035255));
#180426=CARTESIAN_POINT('Ctrl Pts',(17.6343982077823,-20.7610342616876,
18.7565793983152));
#180427=CARTESIAN_POINT('Ctrl Pts',(17.6289945197368,-20.7577386158154,
18.7569585265789));
#180428=CARTESIAN_POINT('Ctrl Pts',(17.6164855843831,-20.7500323879735,
18.7578406668203));
#180429=CARTESIAN_POINT('Ctrl Pts',(17.609391566976,-20.7456038599841,18.7583443370504));
#180430=CARTESIAN_POINT('Ctrl Pts',(17.5945073694618,-20.7361891971656,
18.7594083542173));
#180431=CARTESIAN_POINT('Ctrl Pts',(17.5867232704195,-20.7311938196375,
18.7599690379269));
#180432=CARTESIAN_POINT('Ctrl Pts',(17.5312962851622,-20.6951090519398,
18.7639920475868));
#180433=CARTESIAN_POINT('Ctrl Pts',(17.4848948086058,-20.6621639231155,
18.7675237217266));
#180434=CARTESIAN_POINT('Ctrl Pts',(17.3461891787905,-20.5550237821855,
18.7786068267213));
#180435=CARTESIAN_POINT('Ctrl Pts',(17.25874479068,-20.4749314439539,18.7863698760382));
#180436=CARTESIAN_POINT('Ctrl Pts',(17.091001679314,-20.2932198850077,18.802708512097));
#180437=CARTESIAN_POINT('Ctrl Pts',(17.0123728631016,-20.1906768202147,
18.8112605488916));
#180438=CARTESIAN_POINT('Ctrl Pts',(16.9351302367768,-20.0682464606865,
18.8202923621346));
#180439=CARTESIAN_POINT('Ctrl Pts',(16.9268499817913,-20.0547907469947,
18.8212699336696));
#180440=CARTESIAN_POINT('Ctrl Pts',(16.915733185637,-20.0362640405035,18.8225941057163));
#180441=CARTESIAN_POINT('Ctrl Pts',(16.9127659692592,-20.0312725906094,
18.8229487229113));
#180442=CARTESIAN_POINT('Ctrl Pts',(16.9080867052436,-20.0233268863816,
18.8235097557657));
#180443=CARTESIAN_POINT('Ctrl Pts',(16.9063612281725,-20.0203806332709,
18.823717032333));
#180444=CARTESIAN_POINT('Ctrl Pts',(16.9028150096578,-20.0142917312017,
18.8241438287768));
#180445=CARTESIAN_POINT('Ctrl Pts',(16.9009952269551,-20.0111485699262,
18.8243632811183));
#180446=CARTESIAN_POINT('Ctrl Pts',(16.8966826662816,-20.0036554336294,
18.8248844213262));
#180447=CARTESIAN_POINT('Ctrl Pts',(16.8941972158079,-19.9993012232976,
18.8251856366385));
#180448=CARTESIAN_POINT('Ctrl Pts',(16.8858866529192,-19.9846212316007,
18.8261958838662));
#180449=CARTESIAN_POINT('Ctrl Pts',(16.8801326941077,-19.9742551434205,
18.8269004931045));
#180450=CARTESIAN_POINT('Ctrl Pts',(16.8159013534574,-19.8562125225849,
18.8348315484422));
#180451=CARTESIAN_POINT('Ctrl Pts',(16.7667827704242,-19.7436865297984,
18.841530865915));
#180452=CARTESIAN_POINT('Ctrl Pts',(16.6748842569598,-19.470747069851,18.857190033624));
#180453=CARTESIAN_POINT('Ctrl Pts',(16.6406595988271,-19.3083368764714,
18.8661051454986));
#180454=CARTESIAN_POINT('Ctrl Pts',(16.6232302279499,-19.1165532282056,
18.8772499173543));
#180455=CARTESIAN_POINT('Ctrl Pts',(16.6212927645111,-19.08945847855,18.8788369280021));
#180456=CARTESIAN_POINT('Ctrl Pts',(16.6193445967408,-19.0521296862209,
18.8810434740439));
#180457=CARTESIAN_POINT('Ctrl Pts',(16.6188859028437,-19.041920960038,18.8816489824037));
#180458=CARTESIAN_POINT('Ctrl Pts',(16.6182717243159,-19.0256205837814,
18.8826192351296));
#180459=CARTESIAN_POINT('Ctrl Pts',(16.6180685938325,-19.0195308084167,
18.8829824827062));
#180460=CARTESIAN_POINT('Ctrl Pts',(16.6177137006813,-19.0073076836854,
18.8837131443583));
#180461=CARTESIAN_POINT('Ctrl Pts',(16.6175623044064,-19.0011743835767,
18.884080566321));
#180462=CARTESIAN_POINT('Ctrl Pts',(16.6172825438711,-18.9874168809957,
18.8849065358592));
#180463=CARTESIAN_POINT('Ctrl Pts',(16.6171687078937,-18.9797924976334,
18.8853655343681));
#180464=CARTESIAN_POINT('Ctrl Pts',(16.6170306367622,-18.965299883049,18.8862404332388));
#180465=CARTESIAN_POINT('Ctrl Pts',(16.6169986298212,-18.9584318228613,
18.8866560826862));
#180466=CARTESIAN_POINT('Ctrl Pts',(16.6170000449379,-18.9515638040726,
18.8870727812038));
#180467=CARTESIAN_POINT('Ctrl Pts',(16.6170000447709,-18.9515646150098,
18.8870727320024));
#180468=CARTESIAN_POINT('Ctrl Pts',(16.6170019870511,-18.9421205433658,
18.8876457254658));
#180469=CARTESIAN_POINT('Ctrl Pts',(16.6170671251749,-18.9326766817956,
18.8882206949119));
#180470=CARTESIAN_POINT('Ctrl Pts',(16.6174515758742,-18.9043864311521,
18.8899491569953));
#180471=CARTESIAN_POINT('Ctrl Pts',(16.6179593948816,-18.885543960166,18.891108465017));
#180472=CARTESIAN_POINT('Ctrl Pts',(16.6223792669253,-18.7759249068819,
18.8979010800054));
#180473=CARTESIAN_POINT('Ctrl Pts',(16.631880159825,-18.6854794754026,18.9037040531802));
#180474=CARTESIAN_POINT('Ctrl Pts',(16.6686806511801,-18.4697987853706,
18.9179617591797));
#180475=CARTESIAN_POINT('Ctrl Pts',(16.7015809841445,-18.3459488760637,
18.9265076073661));
#180476=CARTESIAN_POINT('Ctrl Pts',(16.7454194046824,-18.2258896668368,
18.9348454761515));
#180477=CARTESIAN_POINT('Origin',(18.734,-18.952,0.));
#180478=CARTESIAN_POINT('',(16.7454193686617,-18.225889765486,19.9537492327042));
#180479=CARTESIAN_POINT('',(16.7454194015149,-18.2258896755116,19.7345260518445));
#180480=CARTESIAN_POINT('',(16.7454193692319,-18.2258897639242,0.));
#180481=CARTESIAN_POINT('',(16.6200858807113,-18.9511715411787,19.9109956519321));
#180482=CARTESIAN_POINT('Ctrl Pts',(16.7454193686617,-18.225889765486,19.9537492327042));
#180483=CARTESIAN_POINT('Ctrl Pts',(16.7274346678508,-18.2751440329415,
19.9507625194471));
#180484=CARTESIAN_POINT('Ctrl Pts',(16.7112837739167,-18.3250558959446,
19.9478475512712));
#180485=CARTESIAN_POINT('Ctrl Pts',(16.6439835682757,-18.5628628691546,
19.9342646472639));
#180486=CARTESIAN_POINT('Ctrl Pts',(16.6170670032748,-18.7565969919825,
19.9239833310379));
#180487=CARTESIAN_POINT('Ctrl Pts',(16.6170001249218,-18.951272731851,19.9127739724915));
#180488=CARTESIAN_POINT('Ctrl Pts',(16.7477768045735,-18.2267292102227,
19.1554367670381));
#180489=CARTESIAN_POINT('Ctrl Pts',(16.8351529008212,-17.9823751202301,
19.1710019290282));
#180490=CARTESIAN_POINT('Ctrl Pts',(17.3199689890727,-17.1326716746796,
19.2289590265787));
#180491=CARTESIAN_POINT('Ctrl Pts',(19.0938031787897,-16.4747288712945,
19.3293080596899));
#180492=CARTESIAN_POINT('Ctrl Pts',(21.0117476238401,-17.913637640173,19.4564838663712));
#180493=CARTESIAN_POINT('Ctrl Pts',(20.8399999988753,-20.3051794704029,
19.5836596730529));
#180494=CARTESIAN_POINT('Ctrl Pts',(18.7361280843894,-21.4552630390637,
19.7108354797341));
#180495=CARTESIAN_POINT('Ctrl Pts',(16.9296977662697,-20.4717617465338,
19.8199301623759));
#180496=CARTESIAN_POINT('Ctrl Pts',(16.6216055049255,-19.3568003466498,
19.8866329094569));
#180497=CARTESIAN_POINT('Ctrl Pts',(16.6201759917111,-18.9511685861838,
19.9109437209775));
#180498=CARTESIAN_POINT('Ctrl Pts',(16.7454194046824,-18.2258896668368,
18.9348454761515));
#180499=CARTESIAN_POINT('Ctrl Pts',(16.7570884628114,-18.1939319029804,
18.9370648780901));
#180500=CARTESIAN_POINT('Ctrl Pts',(16.7695325581869,-18.1622426395963,
18.9392681509443));
#180501=CARTESIAN_POINT('Ctrl Pts',(16.7978320888527,-18.094995909626,18.9439304994503));
#180502=CARTESIAN_POINT('Ctrl Pts',(16.8139071802867,-18.059561655898,18.946379141603));
#180503=CARTESIAN_POINT('Ctrl Pts',(16.8342943057911,-18.0177272746171,
18.9492432259045));
#180504=CARTESIAN_POINT('Ctrl Pts',(16.8376749300514,-18.0108844474981,
18.949710824525));
#180505=CARTESIAN_POINT('Ctrl Pts',(16.8429711197998,-18.0003086765001,
18.9504319722154));
#180506=CARTESIAN_POINT('Ctrl Pts',(16.8448608599526,-17.9965629737017,
18.950687085914));
#180507=CARTESIAN_POINT('Ctrl Pts',(16.848375936133,-17.9896468514508,18.9511575399267));
#180508=CARTESIAN_POINT('Ctrl Pts',(16.8499981269829,-17.9864749430819,
18.951373067141));
#180509=CARTESIAN_POINT('Ctrl Pts',(16.8536706109008,-17.9793385437404,
18.9518574579925));
#180510=CARTESIAN_POINT('Ctrl Pts',(16.8557254323329,-17.9753764444285,
18.9521260322908));
#180511=CARTESIAN_POINT('Ctrl Pts',(16.8610264414634,-17.9652336718004,
18.9528127264605));
#180512=CARTESIAN_POINT('Ctrl Pts',(16.8642907288321,-17.9590624481791,
18.953229730566));
#180513=CARTESIAN_POINT('Ctrl Pts',(16.8837668644529,-17.9226788929136,
18.9556841506719));
#180514=CARTESIAN_POINT('Ctrl Pts',(16.9006812294319,-17.8928460053321,
18.9576798978954));
#180515=CARTESIAN_POINT('Ctrl Pts',(16.9273135936181,-17.8484241948838,
18.960646065502));
#180516=CARTESIAN_POINT('Ctrl Pts',(16.9364993136674,-17.8335248586289,
18.9616399630232));
#180517=CARTESIAN_POINT('Ctrl Pts',(16.9793498503821,-17.7659124593839,
18.9661536890462));
#180518=CARTESIAN_POINT('Ctrl Pts',(17.0151572734018,-17.7145908870264,
18.9695902490886));
#180519=CARTESIAN_POINT('Ctrl Pts',(17.1378438074485,-17.5543720561936,
18.9805947905333));
#180520=CARTESIAN_POINT('Ctrl Pts',(17.2331970839525,-17.4524442963095,
18.9880574999124));
#180521=CARTESIAN_POINT('Ctrl Pts',(17.3845634027533,-17.3196492618426,
18.9993996751176));
#180522=CARTESIAN_POINT('Ctrl Pts',(17.4330378580147,-17.2807595921025,
19.0029643204398));
#180523=CARTESIAN_POINT('Ctrl Pts',(17.4907758960535,-17.2384737522687,
19.0071712870023));
#180524=CARTESIAN_POINT('Ctrl Pts',(17.4984402103519,-17.2329391005084,
19.0077289452487));
#180525=CARTESIAN_POINT('Ctrl Pts',(17.5128019793564,-17.222713658795,19.0087725980823));
#180526=CARTESIAN_POINT('Ctrl Pts',(17.5194900581518,-17.218009961449,19.0092580879349));
#180527=CARTESIAN_POINT('Ctrl Pts',(17.5314545473805,-17.2096985655876,
19.0101257429806));
#180528=CARTESIAN_POINT('Ctrl Pts',(17.5367203901491,-17.2060757781551,
19.0105073267565));
#180529=CARTESIAN_POINT('Ctrl Pts',(17.5469361783478,-17.1991154847975,
19.0112470798994));
#180530=CARTESIAN_POINT('Ctrl Pts',(17.5518839993482,-17.1957749574213,
19.0116051298251));
#180531=CARTESIAN_POINT('Ctrl Pts',(17.5647943129503,-17.187137819406,19.0125388137285));
#180532=CARTESIAN_POINT('Ctrl Pts',(17.5727786175947,-17.1818741989703,
19.0131156816155));
#180533=CARTESIAN_POINT('Ctrl Pts',(17.6001202371883,-17.1641139434264,
19.015089383579));
#180534=CARTESIAN_POINT('Ctrl Pts',(17.6196452446085,-17.1518796481589,
19.0164959082361));
#180535=CARTESIAN_POINT('Ctrl Pts',(17.788848981634,-17.0496650427208,19.0286642816667));
#180536=CARTESIAN_POINT('Ctrl Pts',(17.9489055021189,-16.9782238591999,
19.0401221716249));
#180537=CARTESIAN_POINT('Ctrl Pts',(18.1996624686206,-16.901671424279,19.0574454787337));
#180538=CARTESIAN_POINT('Ctrl Pts',(18.2849636857144,-16.8813160099883,
19.0632207210498));
#180539=CARTESIAN_POINT('Ctrl Pts',(18.4086969013825,-16.8597980877337,
19.0712401370994));
#180540=CARTESIAN_POINT('Ctrl Pts',(18.4462794366656,-16.8542992969227,
19.0736289775107));
#180541=CARTESIAN_POINT('Ctrl Pts',(18.4915193594574,-16.8489190220765,
19.0764325174345));
#180542=CARTESIAN_POINT('Ctrl Pts',(18.4990514862175,-16.8480642451338,
19.0768969000997));
#180543=CARTESIAN_POINT('Ctrl Pts',(18.5107480644012,-16.8468004655189,
19.0776141632025));
#180544=CARTESIAN_POINT('Ctrl Pts',(18.5149093224702,-16.8463633308553,
19.0778685820089));
#180545=CARTESIAN_POINT('Ctrl Pts',(18.5226170493732,-16.8455767407218,
19.0783383903923));
#180546=CARTESIAN_POINT('Ctrl Pts',(18.5261630740572,-16.8452239056892,
19.0785539627899));
#180547=CARTESIAN_POINT('Ctrl Pts',(18.5341667015867,-16.8444479362959,
19.0790392551567));
#180548=CARTESIAN_POINT('Ctrl Pts',(18.5386247531142,-16.8440299902206,
19.0793086809283));
#180549=CARTESIAN_POINT('Ctrl Pts',(18.5517426478401,-16.8428421486321,
19.0800989592126));
#180550=CARTESIAN_POINT('Ctrl Pts',(18.5604060672873,-16.8421114397183,
19.0806176627257));
#180551=CARTESIAN_POINT('Ctrl Pts',(18.621734271462,-16.8373190658068,19.0842683445178));
#180552=CARTESIAN_POINT('Ctrl Pts',(18.6745350045372,-16.8351759746401,
19.087300940387));
#180553=CARTESIAN_POINT('Ctrl Pts',(18.7465911725506,-16.8349501398834,
19.0913550533332));
#180554=CARTESIAN_POINT('Ctrl Pts',(18.7658176456134,-16.8351517965832,
19.0924285875697));
#180555=CARTESIAN_POINT('Ctrl Pts',(18.9163107073358,-16.8387811128402,
19.1007848648068));
#180556=CARTESIAN_POINT('Ctrl Pts',(19.0470061788596,-16.8541532531974,
19.1077814410658));
#180557=CARTESIAN_POINT('Ctrl Pts',(19.2706276321882,-16.9018310986907,
19.1203476264407));
#180558=CARTESIAN_POINT('Ctrl Pts',(19.3642927990027,-16.9286637675744,
19.1257988761686));
#180559=CARTESIAN_POINT('Ctrl Pts',(19.4760991229478,-16.9692127324013,
19.13272265801));
#180560=CARTESIAN_POINT('Ctrl Pts',(19.4963097525252,-16.9768948769489,
19.133991102269));
#180561=CARTESIAN_POINT('Ctrl Pts',(19.5248063821402,-16.9882291022287,
19.1358050821958));
#180562=CARTESIAN_POINT('Ctrl Pts',(19.5331924922735,-16.9916270177871,
19.1363420724951));
#180563=CARTESIAN_POINT('Ctrl Pts',(19.5475959053332,-16.9975708278052,
19.1372699398318));
#180564=CARTESIAN_POINT('Ctrl Pts',(19.5536237242554,-17.0000910278747,
19.1376599422343));
#180565=CARTESIAN_POINT('Ctrl Pts',(19.5651249942043,-17.0049623194101,
19.1384073568916));
#180566=CARTESIAN_POINT('Ctrl Pts',(19.570600385019,-17.0073086928032,19.1387646054515));
#180567=CARTESIAN_POINT('Ctrl Pts',(19.5847740770105,-17.0134534934314,
19.1396931323328));
#180568=CARTESIAN_POINT('Ctrl Pts',(19.5934567955743,-17.0172873339447,
19.1402656177185));
#180569=CARTESIAN_POINT('Ctrl Pts',(19.6227796478703,-17.0304711371218,
19.1422116434207));
#180570=CARTESIAN_POINT('Ctrl Pts',(19.6432947914618,-17.0400937907563,
19.1435945208269));
#180571=CARTESIAN_POINT('Ctrl Pts',(19.8251074307862,-17.1289613839584,
19.1560466407167));
#180572=CARTESIAN_POINT('Ctrl Pts',(19.9758290028525,-17.2281030094809,
19.1678585491742));
#180573=CARTESIAN_POINT('Ctrl Pts',(20.1760214330389,-17.3997968032999,
19.1852794517686));
#180574=CARTESIAN_POINT('Ctrl Pts',(20.2365392085328,-17.4583004514745,
19.1908145653132));
#180575=CARTESIAN_POINT('Ctrl Pts',(20.3184928357187,-17.5475620548898,
19.1985462418226));
#180576=CARTESIAN_POINT('Ctrl Pts',(20.3428465080606,-17.5755274105513,
19.2008771376845));
#180577=CARTESIAN_POINT('Ctrl Pts',(20.3712479842207,-17.6099252197752,
19.2036218635466));
#180578=CARTESIAN_POINT('Ctrl Pts',(20.3760103807324,-17.6157561633335,
19.2040830333732));
#180579=CARTESIAN_POINT('Ctrl Pts',(20.3833639932923,-17.6248583985714,
19.2047964138572));
#180580=CARTESIAN_POINT('Ctrl Pts',(20.3859767582418,-17.628112088002,19.2050501368392));
#180581=CARTESIAN_POINT('Ctrl Pts',(20.3908035467717,-17.6341594506911,
19.2055193042174));
#180582=CARTESIAN_POINT('Ctrl Pts',(20.3930201151048,-17.636950965186,19.2057349273356));
#180583=CARTESIAN_POINT('Ctrl Pts',(20.3980142547639,-17.6432732369954,
19.2062211473178));
#180584=CARTESIAN_POINT('Ctrl Pts',(20.4007876371128,-17.6468072349708,
19.206491445015));
#180585=CARTESIAN_POINT('Ctrl Pts',(20.4079005676947,-17.6559305725278,
19.2071854994357));
#180586=CARTESIAN_POINT('Ctrl Pts',(20.4122234191288,-17.6615329411301,
19.2076080995231));
#180587=CARTESIAN_POINT('Ctrl Pts',(20.4382099911459,-17.6955626851827,
19.2101540703532));
#180588=CARTESIAN_POINT('Ctrl Pts',(20.4591804384396,-17.7245150862502,
19.2122321053226));
#180589=CARTESIAN_POINT('Ctrl Pts',(20.4908383183962,-17.7706380626517,
19.2154308753774));
#180590=CARTESIAN_POINT('Ctrl Pts',(20.5020290720741,-17.7874528134322,
19.2165746493271));
#180591=CARTESIAN_POINT('Ctrl Pts',(20.5195033725233,-17.8145415947981,
19.2183861563385));
#180592=CARTESIAN_POINT('Ctrl Pts',(20.525942642236,-17.8247132167781,19.219059498116));
#180593=CARTESIAN_POINT('Ctrl Pts',(20.6129380321566,-17.9647623394819,
19.2282445481));
#180594=CARTESIAN_POINT('Ctrl Pts',(20.6792881132402,-18.1029389149436,
19.236334340286));
#180595=CARTESIAN_POINT('Ctrl Pts',(20.7506393516376,-18.3049850530612,
19.2481914398177));
#180596=CARTESIAN_POINT('Ctrl Pts',(20.7685626158003,-18.3637681306169,
19.2516394576249));
#180597=CARTESIAN_POINT('Ctrl Pts',(20.7931692537302,-18.4591642522932,
19.2572939947741));
#180598=CARTESIAN_POINT('Ctrl Pts',(20.801488339313,-18.4953197946267,19.2594500538526));
#180599=CARTESIAN_POINT('Ctrl Pts',(20.8110603208846,-18.5425698803645,
19.2622919772058));
#180600=CARTESIAN_POINT('Ctrl Pts',(20.8131817854244,-18.5534831302344,
19.2629500240045));
#180601=CARTESIAN_POINT('Ctrl Pts',(20.8164925494308,-18.5712608387683,
19.2640248641374));
#180602=CARTESIAN_POINT('Ctrl Pts',(20.817734114491,-18.5781154380642,19.2644399870978));
#180603=CARTESIAN_POINT('Ctrl Pts',(20.8200569496059,-18.5913106944204,
19.2652404915197));
#180604=CARTESIAN_POINT('Ctrl Pts',(20.8211431995176,-18.5976504050376,
19.265625709593));
#180605=CARTESIAN_POINT('Ctrl Pts',(20.8235645518027,-18.6121797016758,
19.2665099935391));
#180606=CARTESIAN_POINT('Ctrl Pts',(20.8248804239037,-18.6203723455762,
19.2670096643233));
#180607=CARTESIAN_POINT('Ctrl Pts',(20.8282490302082,-18.6421627671133,
19.2683415437393));
#180608=CARTESIAN_POINT('Ctrl Pts',(20.8302174652415,-18.6557729995072,
19.2691764057548));
#180609=CARTESIAN_POINT('Ctrl Pts',(20.8442539650008,-18.7599819410745,
19.2755923397658));
#180610=CARTESIAN_POINT('Ctrl Pts',(20.8505744557554,-18.8512456133866,
19.2813542853221));
#180611=CARTESIAN_POINT('Ctrl Pts',(20.8516030981444,-19.0834590446548,
19.2963554179827));
#180612=CARTESIAN_POINT('Ctrl Pts',(20.8381706346522,-19.2240026311207,
19.3057703904286));
#180613=CARTESIAN_POINT('Ctrl Pts',(20.8005242380613,-19.4146312952238,
19.3184843007429));
#180614=CARTESIAN_POINT('Ctrl Pts',(20.7881750889048,-19.4666995468883,
19.3219468570176));
#180615=CARTESIAN_POINT('Ctrl Pts',(20.7664135033988,-19.5450941272576,
19.3270930822964));
#180616=CARTESIAN_POINT('Ctrl Pts',(20.7584313696157,-19.571792784749,19.328833542518));
#180617=CARTESIAN_POINT('Ctrl Pts',(20.7478193396684,-19.604892174682,19.3309693567385));
#180618=CARTESIAN_POINT('Ctrl Pts',(20.745682549206,-19.6114466231811,19.3313912148695));
#180619=CARTESIAN_POINT('Ctrl Pts',(20.742244921945,-19.6218190804271,19.3320569578469));
#180620=CARTESIAN_POINT('Ctrl Pts',(20.7409651477704,-19.6256439439981,
19.332302051663));
#180621=CARTESIAN_POINT('Ctrl Pts',(20.7385269507804,-19.6328623659053,
19.3327638133681));
#180622=CARTESIAN_POINT('Ctrl Pts',(20.7373708515019,-19.6362565960473,
19.3329806078123));
#180623=CARTESIAN_POINT('Ctrl Pts',(20.734702778814,-19.6440251518377,19.3334760528216));
#180624=CARTESIAN_POINT('Ctrl Pts',(20.7331850824364,-19.6483974633965,
19.3337543612437));
#180625=CARTESIAN_POINT('Ctrl Pts',(20.7291068209342,-19.6600232633561,
19.3344930240172));
#180626=CARTESIAN_POINT('Ctrl Pts',(20.7265210136035,-19.6672679098113,
19.3349519231628));
#180627=CARTESIAN_POINT('Ctrl Pts',(20.7078196339748,-19.7187750054841,
19.3382056304466));
#180628=CARTESIAN_POINT('Ctrl Pts',(20.6902688878991,-19.7625063981389,
19.3409211871729));
#180629=CARTESIAN_POINT('Ctrl Pts',(20.669489497135,-19.8096648249915,19.3438351235066));
#180630=CARTESIAN_POINT('Ctrl Pts',(20.6676941633895,-19.8137049544192,
19.3440846459375));
#180631=CARTESIAN_POINT('Ctrl Pts',(20.6408105238953,-19.8736954415322,
19.3477883652465));
#180632=CARTESIAN_POINT('Ctrl Pts',(20.6133142530743,-19.9285385677627,
19.3511573717879));
#180633=CARTESIAN_POINT('Ctrl Pts',(20.5796910269915,-19.9889060188677,
19.3549257229204));
#180634=CARTESIAN_POINT('Ctrl Pts',(20.5758701114349,-19.9956780884566,
19.3553493252538));
#180635=CARTESIAN_POINT('Ctrl Pts',(20.5178668649513,-20.0971705871352,
19.3617128901422));
#180636=CARTESIAN_POINT('Ctrl Pts',(20.4564780317384,-20.1875829336354,
19.367589847347));
#180637=CARTESIAN_POINT('Ctrl Pts',(20.341388233038,-20.3317349235385,19.3778487607524));
#180638=CARTESIAN_POINT('Ctrl Pts',(20.2912750959758,-20.3880563862115,
19.3821205113765));
#180639=CARTESIAN_POINT('Ctrl Pts',(20.2250080929037,-20.4549767563713,
19.3876192914436));
#180640=CARTESIAN_POINT('Ctrl Pts',(20.2115678395912,-20.4681917783405,
19.3887272856715));
#180641=CARTESIAN_POINT('Ctrl Pts',(20.1917685395629,-20.4871459834144,
19.3903500300447));
#180642=CARTESIAN_POINT('Ctrl Pts',(20.1855480526442,-20.4930290564791,
19.3908585292913));
#180643=CARTESIAN_POINT('Ctrl Pts',(20.1745788286112,-20.503277939913,19.3917529902637));
#180644=CARTESIAN_POINT('Ctrl Pts',(20.1698454771274,-20.5076601083446,
19.3921382435731));
#180645=CARTESIAN_POINT('Ctrl Pts',(20.1606151615669,-20.5161275819359,
19.392888161763));
#180646=CARTESIAN_POINT('Ctrl Pts',(20.1561204887208,-20.5202152996795,
19.3932527185138));
#180647=CARTESIAN_POINT('Ctrl Pts',(20.145332999645,-20.5299415567236,19.3941262517233));
#180648=CARTESIAN_POINT('Ctrl Pts',(20.1390239366184,-20.5355618480545,
19.3946359892651));
#180649=CARTESIAN_POINT('Ctrl Pts',(20.1161323168404,-20.5557098530103,
19.3964815111889));
#180650=CARTESIAN_POINT('Ctrl Pts',(20.0993571637733,-20.5700156957051,
19.3978264467296));
#180651=CARTESIAN_POINT('Ctrl Pts',(19.9387773062635,-20.7026825455715,
19.4106353225211));
#180652=CARTESIAN_POINT('Ctrl Pts',(19.7801908653824,-20.8018201292752,
19.4229050703923));
#180653=CARTESIAN_POINT('Ctrl Pts',(19.5381705459434,-20.9119372376495,
19.4404587862508));
#180654=CARTESIAN_POINT('Ctrl Pts',(19.4637964908475,-20.9408295622266,
19.4456955606116));
#180655=CARTESIAN_POINT('Ctrl Pts',(19.3538078145852,-20.9765535584202,
19.453066728074));
#180656=CARTESIAN_POINT('Ctrl Pts',(19.3193708288086,-20.9867776747693,
19.4553229482392));
#180657=CARTESIAN_POINT('Ctrl Pts',(19.277485639458,-20.9980615827153,19.4579916528729));
#180658=CARTESIAN_POINT('Ctrl Pts',(19.2702728392629,-20.9999638879231,
19.4584485348146));
#180659=CARTESIAN_POINT('Ctrl Pts',(19.2590241650428,-21.0028671125153,
19.4591567307659));
#180660=CARTESIAN_POINT('Ctrl Pts',(19.2549952249584,-21.0038943109558,
19.4594095226368));
#180661=CARTESIAN_POINT('Ctrl Pts',(19.24750520083,-21.0057804471485,19.4598778411388));
#180662=CARTESIAN_POINT('Ctrl Pts',(19.2440450057794,-21.0066425014399,
19.4600935409866));
#180663=CARTESIAN_POINT('Ctrl Pts',(19.2362012187612,-21.0085756241998,
19.4605810425862));
#180664=CARTESIAN_POINT('Ctrl Pts',(19.2318163818485,-21.0096414199291,
19.4608525383525));
#180665=CARTESIAN_POINT('Ctrl Pts',(19.2204825495345,-21.0123579158214,
19.4615517217026));
#180666=CARTESIAN_POINT('Ctrl Pts',(19.2135284834494,-21.0139874997492,
19.4619782237731));
#180667=CARTESIAN_POINT('Ctrl Pts',(19.170699692491,-21.023795416176,19.464590392434));
#180668=CARTESIAN_POINT('Ctrl Pts',(19.1346226855039,-21.0310730384115,
19.4667279698121));
#180669=CARTESIAN_POINT('Ctrl Pts',(18.9307620373476,-21.066692512723,19.4785481229896));
#180670=CARTESIAN_POINT('Ctrl Pts',(18.7602181738375,-21.0756676543417,
19.4875020264752));
#180671=CARTESIAN_POINT('Ctrl Pts',(18.4950675593476,-21.0576437212988,
19.5021198005965));
#180672=CARTESIAN_POINT('Ctrl Pts',(18.4002682668898,-21.0447121721664,
19.5074782474928));
#180673=CARTESIAN_POINT('Ctrl Pts',(18.2857006089707,-21.0211000927665,
19.5142895682617));
#180674=CARTESIAN_POINT('Ctrl Pts',(18.2647952826919,-21.0164598377371,
19.5155460334569));
#180675=CARTESIAN_POINT('Ctrl Pts',(18.2351957815223,-21.0094169715902,
19.5173458095867));
#180676=CARTESIAN_POINT('Ctrl Pts',(18.2264405937413,-21.0072746017626,
19.517880758738));
#180677=CARTESIAN_POINT('Ctrl Pts',(18.2113694488999,-21.003484562464,19.5188062060002));
#180678=CARTESIAN_POINT('Ctrl Pts',(18.2050468930286,-21.001863461825,19.5191958415977));
#180679=CARTESIAN_POINT('Ctrl Pts',(18.1929617050235,-20.9987051896961,
19.5199433239361));
#180680=CARTESIAN_POINT('Ctrl Pts',(18.1871978655578,-20.9971728520587,
19.5203010107074));
#180681=CARTESIAN_POINT('Ctrl Pts',(18.1722402084362,-20.9931285536587,
19.5212323625708));
#180682=CARTESIAN_POINT('Ctrl Pts',(18.1630568175055,-20.9905788465731,
19.5218072494148));
#180683=CARTESIAN_POINT('Ctrl Pts',(18.1318698663868,-20.981692736647,19.5237702287538));
#180684=CARTESIAN_POINT('Ctrl Pts',(18.109952621851,-20.9750615680731,19.5251678811103));
#180685=CARTESIAN_POINT('Ctrl Pts',(17.9198017559213,-20.9141465473261,
19.5374567768308));
#180686=CARTESIAN_POINT('Ctrl Pts',(17.7589034331837,-20.8393528023252,
19.5490634132886));
#180687=CARTESIAN_POINT('Ctrl Pts',(17.5362480538972,-20.6997114176145,
19.5664271812964));
#180688=CARTESIAN_POINT('Ctrl Pts',(17.4661480575475,-20.649544776782,19.5721005136665));
#180689=CARTESIAN_POINT('Ctrl Pts',(17.3701134078433,-20.5715418365208,
19.5799980714077));
#180690=CARTESIAN_POINT('Ctrl Pts',(17.3415659457476,-20.5470643260711,
19.5823625497969));
#180691=CARTESIAN_POINT('Ctrl Pts',(17.3080786349526,-20.5167665622721,
19.5851413803673));
#180692=CARTESIAN_POINT('Ctrl Pts',(17.3025006794945,-20.5116652952008,
19.5856044240878));
#180693=CARTESIAN_POINT('Ctrl Pts',(17.2938810851329,-20.503697128483,19.5863200693361));
#180694=CARTESIAN_POINT('Ctrl Pts',(17.2908204773602,-20.5008509720533,
19.5865741983557));
#180695=CARTESIAN_POINT('Ctrl Pts',(17.285165605735,-20.4955610126774,19.5870437391401));
#180696=CARTESIAN_POINT('Ctrl Pts',(17.2825691070287,-20.4931197439159,
19.58725933202));
#180697=CARTESIAN_POINT('Ctrl Pts',(17.2767199481496,-20.4875923786542,
19.5877450077469));
#180698=CARTESIAN_POINT('Ctrl Pts',(17.2734709288942,-20.4845025077327,
19.5880147943394));
#180699=CARTESIAN_POINT('Ctrl Pts',(17.2639304891813,-20.475371494255,19.5888071133393));
#180700=CARTESIAN_POINT('Ctrl Pts',(17.2576664704176,-20.4693016811104,
19.5893274800962));
#180701=CARTESIAN_POINT('Ctrl Pts',(17.2133360562671,-20.4258112145312,
19.5930127545472));
#180702=CARTESIAN_POINT('Ctrl Pts',(17.1766560709689,-20.3869979909057,
19.5960761544868));
#180703=CARTESIAN_POINT('Ctrl Pts',(17.1324659651828,-20.3365450123097,
19.5998478774551));
#180704=CARTESIAN_POINT('Ctrl Pts',(17.1235520738394,-20.3261665271839,
19.6006131076102));
#180705=CARTESIAN_POINT('Ctrl Pts',(17.0811100918862,-20.275770895466,19.6042820088651));
#180706=CARTESIAN_POINT('Ctrl Pts',(17.0489682591895,-20.2346078308291,
19.6071384935807));
#180707=CARTESIAN_POINT('Ctrl Pts',(16.9542697434346,-20.1036177398395,
19.6159390347208));
#180708=CARTESIAN_POINT('Ctrl Pts',(16.8971322474374,-20.0101016915657,
19.6218308906142));
#180709=CARTESIAN_POINT('Ctrl Pts',(16.8130787470599,-19.8450279892142,
19.6321302016449));
#180710=CARTESIAN_POINT('Ctrl Pts',(16.7823335280967,-19.7756708576587,
19.6364278337816));
#180711=CARTESIAN_POINT('Ctrl Pts',(16.7486505846779,-19.6871424284868,
19.6419578080245));
#180712=CARTESIAN_POINT('Ctrl Pts',(16.7421624440022,-19.6693770328492,
19.6430695285059));
#180713=CARTESIAN_POINT('Ctrl Pts',(16.7330803286727,-19.6434354462674,
19.6446967392415));
#180714=CARTESIAN_POINT('Ctrl Pts',(16.7302965253059,-19.6353263419915,
19.6452059293288));
#180715=CARTESIAN_POINT('Ctrl Pts',(16.7255041824423,-19.6210853329903,
19.646101189266));
#180716=CARTESIAN_POINT('Ctrl Pts',(16.7234742631018,-19.6149607015629,
19.6464865467384));
#180717=CARTESIAN_POINT('Ctrl Pts',(16.7195884541053,-19.6030545244012,
19.6472363587356));
#180718=CARTESIAN_POINT('Ctrl Pts',(16.7177293756182,-19.5972740797814,
19.6476007036782));
#180719=CARTESIAN_POINT('Ctrl Pts',(16.7133468281112,-19.5834435293021,
19.6484732305761));
#180720=CARTESIAN_POINT('Ctrl Pts',(16.7108465750517,-19.5753862267157,
19.6489821696574));
#180721=CARTESIAN_POINT('Ctrl Pts',(16.7020108021448,-19.5462989944584,
19.6508218507045));
#180722=CARTESIAN_POINT('Ctrl Pts',(16.6959546563939,-19.5251862833178,
19.652161668566));
#180723=CARTESIAN_POINT('Ctrl Pts',(16.641457713617,-19.3234062371902,19.6650134940398));
#180724=CARTESIAN_POINT('Ctrl Pts',(16.6168436525179,-19.1371933084926,
19.6773392583007));
#180725=CARTESIAN_POINT('Ctrl Pts',(16.6170536900537,-18.8872094297229,
19.6938412674434));
#180726=CARTESIAN_POINT('Ctrl Pts',(16.6199199093975,-18.8242283085218,
19.6979837633764));
#180727=CARTESIAN_POINT('Ctrl Pts',(16.6300811408892,-18.711786107144,19.7052635121147));
#180728=CARTESIAN_POINT('Ctrl Pts',(16.636325596411,-18.6622755733997,19.7084278670485));
#180729=CARTESIAN_POINT('Ctrl Pts',(16.6455655237967,-18.6053135180284,
19.7119866163342));
#180730=CARTESIAN_POINT('Ctrl Pts',(16.6468596259147,-18.5976059518692,
19.712466400274));
#180731=CARTESIAN_POINT('Ctrl Pts',(16.6489941842261,-18.5853100717682,
19.7132288067553));
#180732=CARTESIAN_POINT('Ctrl Pts',(16.6498071586553,-18.5807171478172,
19.7135129229699));
#180733=CARTESIAN_POINT('Ctrl Pts',(16.6512728103078,-18.5725934303284,
19.7140142235687));
#180734=CARTESIAN_POINT('Ctrl Pts',(16.6519192986505,-18.5690615642145,
19.7142317557005));
#180735=CARTESIAN_POINT('Ctrl Pts',(16.6533073565544,-18.5615858265706,
19.7146913063151));
#180736=CARTESIAN_POINT('Ctrl Pts',(16.6540511534419,-18.5576424216259,
19.7149331963715));
#180737=CARTESIAN_POINT('Ctrl Pts',(16.6560859627734,-18.5470203405586,
19.7155834147478));
#180738=CARTESIAN_POINT('Ctrl Pts',(16.6573979718081,-18.5403456667975,
19.7159905631367));
#180739=CARTESIAN_POINT('Ctrl Pts',(16.6640292673832,-18.5074484580789,
19.7179906947645));
#180740=CARTESIAN_POINT('Ctrl Pts',(16.66981344442,-18.4813207867021,19.7195586388828));
#180741=CARTESIAN_POINT('Ctrl Pts',(16.6879077563223,-18.4063518552391,
19.7240162613594));
#180742=CARTESIAN_POINT('Ctrl Pts',(16.7014678343997,-18.3578291157312,
19.7268505474143));
#180743=CARTESIAN_POINT('Ctrl Pts',(16.7257202842388,-18.2816443291298,
19.7312843014982));
#180744=CARTESIAN_POINT('Ctrl Pts',(16.7352803842117,-18.2536571543875,
19.7329094646234));
#180745=CARTESIAN_POINT('Ctrl Pts',(16.7454194015149,-18.2258896755116,
19.7345260518445));
#180746=CARTESIAN_POINT('Origin',(18.734,-18.952,0.));
#180747=CARTESIAN_POINT('',(16.7454193641621,-18.2258897778089,20.7554136941352));
#180748=CARTESIAN_POINT('',(16.7454193692319,-18.2258897639242,20.5336910470276));
#180749=CARTESIAN_POINT('',(16.7454193692319,-18.2258897639242,0.));
#180750=CARTESIAN_POINT('Ctrl Pts',(16.7454193641621,-18.2258897778089,
20.7554136941352));
#180751=CARTESIAN_POINT('Ctrl Pts',(16.7360405261122,-18.2515753764448,
20.7536067807895));
#180752=CARTESIAN_POINT('Ctrl Pts',(16.7271552302181,-18.2774539415413,
20.7517981597966));
#180753=CARTESIAN_POINT('Ctrl Pts',(16.6954799886096,-18.3758873131554,
20.7449760055346));
#180754=CARTESIAN_POINT('Ctrl Pts',(16.6761041931915,-18.4494703059319,
20.7399903665825));
#180755=CARTESIAN_POINT('Ctrl Pts',(16.6536719553266,-18.5581190720105,
20.7329253955474));
#180756=CARTESIAN_POINT('Ctrl Pts',(16.647461042645,-18.5924691027361,20.7307344389072));
#180757=CARTESIAN_POINT('Ctrl Pts',(16.6409663520166,-18.6342676419938,
20.7281324118738));
#180758=CARTESIAN_POINT('Ctrl Pts',(16.6398690487731,-18.6415821111108,
20.7276794391764));
#180759=CARTESIAN_POINT('Ctrl Pts',(16.6382167997033,-18.6530034304887,
20.7269759827501));
#180760=CARTESIAN_POINT('Ctrl Pts',(16.6376355527073,-18.6571063309721,
20.7267240521062));
#180761=CARTESIAN_POINT('Ctrl Pts',(16.6365763773783,-18.6647442403221,
20.7262565330955));
#180762=CARTESIAN_POINT('Ctrl Pts',(16.636095341283,-18.6682787152918,20.7260407764863));
#180763=CARTESIAN_POINT('Ctrl Pts',(16.6350235902585,-18.6763053163347,
20.7255521289721));
#180764=CARTESIAN_POINT('Ctrl Pts',(16.6344383625037,-18.6807981222718,
20.7252795503376));
#180765=CARTESIAN_POINT('Ctrl Pts',(16.6327408114509,-18.6941651491507,
20.7244712651555));
#180766=CARTESIAN_POINT('Ctrl Pts',(16.6316702790213,-18.7030447059475,
20.723937857342));
#180767=CARTESIAN_POINT('Ctrl Pts',(16.6239226589407,-18.7709248029828,
20.7198853023156));
#180768=CARTESIAN_POINT('Ctrl Pts',(16.6196735652526,-18.8301816903796,
20.7164920546517));
#180769=CARTESIAN_POINT('Ctrl Pts',(16.6173229632376,-18.9098229033458,
20.7120327871221));
#180770=CARTESIAN_POINT('Ctrl Pts',(16.6170159593102,-18.9301096100837,
20.710905713788));
#180771=CARTESIAN_POINT('Ctrl Pts',(16.6168948154608,-19.0901947037228,
20.7020607995078));
#180772=CARTESIAN_POINT('Ctrl Pts',(16.6306360858099,-19.229658600869,20.694625739485));
#180773=CARTESIAN_POINT('Ctrl Pts',(16.6757501965833,-19.4554694899002,
20.6818794970703));
#180774=CARTESIAN_POINT('Ctrl Pts',(16.6991411812998,-19.5429488037882,
20.6767638054007));
#180775=CARTESIAN_POINT('Ctrl Pts',(16.7324404003773,-19.6416641112144,
20.6706560419502));
#180776=CARTESIAN_POINT('Ctrl Pts',(16.7369541278898,-19.6546273468824,
20.6698472702452));
#180777=CARTESIAN_POINT('Ctrl Pts',(16.744395444465,-19.6753473798551,20.668543378264));
#180778=CARTESIAN_POINT('Ctrl Pts',(16.7472431360756,-19.6831326008422,
20.6680509120219));
#180779=CARTESIAN_POINT('Ctrl Pts',(16.7523808194746,-19.6969266888519,
20.6671737261315));
#180780=CARTESIAN_POINT('Ctrl Pts',(16.7546526140128,-19.7029422564798,
20.6667896188495));
#180781=CARTESIAN_POINT('Ctrl Pts',(16.7594433811066,-19.7154551187021,
20.6659873301412));
#180782=CARTESIAN_POINT('Ctrl Pts',(16.7619670948556,-19.7219505040645,
20.6655689931112));
#180783=CARTESIAN_POINT('Ctrl Pts',(16.7686050596548,-19.7387881655782,
20.664479630898));
#180784=CARTESIAN_POINT('Ctrl Pts',(16.7727688488811,-19.7491105654152,
20.6638069414727));
#180785=CARTESIAN_POINT('Ctrl Pts',(16.791211431219,-19.7938119548698,20.6608723687528));
#180786=CARTESIAN_POINT('Ctrl Pts',(16.8063135223803,-19.8278420853112,
20.6585827070948));
#180787=CARTESIAN_POINT('Ctrl Pts',(16.848825701507,-19.9172037082198,20.6524167066109));
#180788=CARTESIAN_POINT('Ctrl Pts',(16.877770968577,-19.9717612418196,20.648490595315));
#180789=CARTESIAN_POINT('Ctrl Pts',(16.9832805763926,-20.151215140557,20.6350415616405));
#180790=CARTESIAN_POINT('Ctrl Pts',(17.0704030639735,-20.26941241792,20.6252363404938));
#180791=CARTESIAN_POINT('Ctrl Pts',(17.1821608935758,-20.3920922095799,
20.6144037584348));
#180792=CARTESIAN_POINT('Ctrl Pts',(17.1955082976187,-20.4063429784161,
20.6131348438654));
#180793=CARTESIAN_POINT('Ctrl Pts',(17.2456829975289,-20.4584496691791,
20.6084613702613));
#180794=CARTESIAN_POINT('Ctrl Pts',(17.2837289770879,-20.4951114915215,
20.6051052078539));
#180795=CARTESIAN_POINT('Ctrl Pts',(17.3295906236418,-20.5361082253448,
20.6013107228966));
#180796=CARTESIAN_POINT('Ctrl Pts',(17.3361072840997,-20.5418617948689,
20.6007772011702));
#180797=CARTESIAN_POINT('Ctrl Pts',(17.346033606484,-20.5505175425291,20.5999732956802));
#180798=CARTESIAN_POINT('Ctrl Pts',(17.3494172471693,-20.5534492326387,
20.599700790427));
#180799=CARTESIAN_POINT('Ctrl Pts',(17.355510653302,-20.558694998497,20.5992128261721));
#180800=CARTESIAN_POINT('Ctrl Pts',(17.3582169706351,-20.5610129750384,
20.5989970811374));
#180801=CARTESIAN_POINT('Ctrl Pts',(17.3641139142323,-20.5660379857098,
20.5985291096706));
#180802=CARTESIAN_POINT('Ctrl Pts',(17.3673067068545,-20.5687423884035,
20.5982770759103));
#180803=CARTESIAN_POINT('Ctrl Pts',(17.3763062268267,-20.5763195743023,
20.5975703608943));
#180804=CARTESIAN_POINT('Ctrl Pts',(17.382131205714,-20.5811707179265,20.5971172355403));
#180805=CARTESIAN_POINT('Ctrl Pts',(17.4172900636395,-20.6101332159044,
20.5944070748481));
#180806=CARTESIAN_POINT('Ctrl Pts',(17.447244237378,-20.633484709794,20.5922013749046));
#180807=CARTESIAN_POINT('Ctrl Pts',(17.5483208820626,-20.7079974955783,
20.5850329550837));
#180808=CARTESIAN_POINT('Ctrl Pts',(17.6219933520663,-20.7555536645223,
20.5802385223341));
#180809=CARTESIAN_POINT('Ctrl Pts',(17.8507216074712,-20.8838401976737,
20.5659712699388));
#180810=CARTESIAN_POINT('Ctrl Pts',(18.0130032845019,-20.9500851497846,
20.5565783776766));
#180811=CARTESIAN_POINT('Ctrl Pts',(18.2038289333754,-21.0016680788527,
20.545092520438));
#180812=CARTESIAN_POINT('Ctrl Pts',(18.2261825268263,-21.0073203998097,
20.5437418100362));
#180813=CARTESIAN_POINT('Ctrl Pts',(18.2579259868271,-21.0147975844692,
20.5418145682959));
#180814=CARTESIAN_POINT('Ctrl Pts',(18.2672432333167,-21.01692577511,20.5412477863095));
#180815=CARTESIAN_POINT('Ctrl Pts',(18.282402575048,-21.0202805409891,20.5403237114761));
#180816=CARTESIAN_POINT('Ctrl Pts',(18.2882360759247,-21.0215456393437,
20.539967658485));
#180817=CARTESIAN_POINT('Ctrl Pts',(18.3004558097034,-21.0241416433151,
20.5392208255046));
#180818=CARTESIAN_POINT('Ctrl Pts',(18.3068429912705,-21.0254677338496,
20.5388298955966));
#180819=CARTESIAN_POINT('Ctrl Pts',(18.3220483189512,-21.0285513864757,
20.5378978604684));
#180820=CARTESIAN_POINT('Ctrl Pts',(18.3308716806875,-21.0302823202017,
20.5373559108675));
#180821=CARTESIAN_POINT('Ctrl Pts',(18.3606151200208,-21.0359207390981,
20.535525135629));
#180822=CARTESIAN_POINT('Ctrl Pts',(18.3815824968738,-21.03956886522,20.5342280990653));
#180823=CARTESIAN_POINT('Ctrl Pts',(18.5599655130168,-21.0678418563937,
20.523135304694));
#180824=CARTESIAN_POINT('Ctrl Pts',(18.7196138749804,-21.074934203009,20.5127665038184));
#180825=CARTESIAN_POINT('Ctrl Pts',(19.009873038063,-21.0550736888552,20.4935483241033));
#180826=CARTESIAN_POINT('Ctrl Pts',(19.140118218806,-21.0338498936931,20.4848060784439));
#180827=CARTESIAN_POINT('Ctrl Pts',(19.2827905059857,-20.9966921067133,
20.4756083477493));
#180828=CARTESIAN_POINT('Ctrl Pts',(19.2979807394426,-20.9925544809781,
20.4746342744521));
#180829=CARTESIAN_POINT('Ctrl Pts',(19.3187012775334,-20.9866614065457,
20.4733140432787));
#180830=CARTESIAN_POINT('Ctrl Pts',(19.3242721829649,-20.98505223127,20.4729599299371));
#180831=CARTESIAN_POINT('Ctrl Pts',(19.3331114259021,-20.9824595901719,
20.4723994844782));
#180832=CARTESIAN_POINT('Ctrl Pts',(19.3363840699121,-20.9814910890827,
20.4721922947902));
#180833=CARTESIAN_POINT('Ctrl Pts',(19.3431356594666,-20.9794752644625,
20.4717655155514));
#180834=CARTESIAN_POINT('Ctrl Pts',(19.3466142525746,-20.9784268990843,
20.4715459942465));
#180835=CARTESIAN_POINT('Ctrl Pts',(19.3548927264501,-20.975908698818,20.4710244104032));
#180836=CARTESIAN_POINT('Ctrl Pts',(19.3596901480769,-20.9744307253132,
20.4707228225368));
#180837=CARTESIAN_POINT('Ctrl Pts',(19.3758345375252,-20.9693940721196,
20.4697100400223));
#180838=CARTESIAN_POINT('Ctrl Pts',(19.3871570025942,-20.9657567778582,
20.4690032981843));
#180839=CARTESIAN_POINT('Ctrl Pts',(19.5222461879926,-20.9211006942457,
20.4606069815779));
#180840=CARTESIAN_POINT('Ctrl Pts',(19.642017463001,-20.8688212656968,20.4535141585838));
#180841=CARTESIAN_POINT('Ctrl Pts',(19.8982505056643,-20.7275316417389,
20.4376180886874));
#180842=CARTESIAN_POINT('Ctrl Pts',(20.0307851172993,-20.6331701950501,
20.4288393245252));
#180843=CARTESIAN_POINT('Ctrl Pts',(20.1688712790456,-20.5087261798457,
20.4180455884596));
#180844=CARTESIAN_POINT('Ctrl Pts',(20.1862282510867,-20.4925469893425,
20.4166561898094));
#180845=CARTESIAN_POINT('Ctrl Pts',(20.2102696111499,-20.4693696030709,
20.414683107493));
#180846=CARTESIAN_POINT('Ctrl Pts',(20.217183956616,-20.4626117380895,20.4141098213108));
#180847=CARTESIAN_POINT('Ctrl Pts',(20.2283060812245,-20.4515913462797,
20.4131780403851));
#180848=CARTESIAN_POINT('Ctrl Pts',(20.2325425380601,-20.447357860417,20.4128208276019));
#180849=CARTESIAN_POINT('Ctrl Pts',(20.2413435741349,-20.4384880356557,
20.4120738948695));
#180850=CARTESIAN_POINT('Ctrl Pts',(20.2459048526978,-20.4338485231478,
20.4116840353014));
#180851=CARTESIAN_POINT('Ctrl Pts',(20.2566527554761,-20.4228149929531,
20.4107588105762));
#180852=CARTESIAN_POINT('Ctrl Pts',(20.2628205650714,-20.4164028930907,
20.4102226334635));
#180853=CARTESIAN_POINT('Ctrl Pts',(20.2832249136015,-20.3949209760093,
20.4084311950318));
#180854=CARTESIAN_POINT('Ctrl Pts',(20.2972801473271,-20.3796813050984,
20.4071681947257));
#180855=CARTESIAN_POINT('Ctrl Pts',(20.3711099713543,-20.2972322654157,
20.4003745800996));
#180856=CARTESIAN_POINT('Ctrl Pts',(20.4267721943403,-20.2264793467002,
20.3946760389935));
#180857=CARTESIAN_POINT('Ctrl Pts',(20.5545470055131,-20.0408686312935,
20.3800726963549));
#180858=CARTESIAN_POINT('Ctrl Pts',(20.6204508675071,-19.9222194295745,
20.3710222226614));
#180859=CARTESIAN_POINT('Ctrl Pts',(20.7047525840411,-19.7288703172134,
20.3572289567084));
#180860=CARTESIAN_POINT('Ctrl Pts',(20.7312152301385,-19.6580645001745,
20.3523667988651));
#180861=CARTESIAN_POINT('Ctrl Pts',(20.7566813026887,-19.576931562992,20.3471147804785));
#180862=CARTESIAN_POINT('Ctrl Pts',(20.7594632297126,-19.5678553592093,
20.3465316711897));
#180863=CARTESIAN_POINT('Ctrl Pts',(20.7634967477482,-19.5543727474595,
20.3456723340755));
#180864=CARTESIAN_POINT('Ctrl Pts',(20.7647951964889,-19.5499806408494,
20.3453934715943));
#180865=CARTESIAN_POINT('Ctrl Pts',(20.7670808512854,-19.5421559191414,
20.3448986229934));
#180866=CARTESIAN_POINT('Ctrl Pts',(20.7680736320409,-19.5387249925239,
20.3446823154755));
#180867=CARTESIAN_POINT('Ctrl Pts',(20.7701902917305,-19.5313401347524,
20.3442181754018));
#180868=CARTESIAN_POINT('Ctrl Pts',(20.7713113362327,-19.5273854497558,
20.3439705085504));
#180869=CARTESIAN_POINT('Ctrl Pts',(20.7743760289068,-19.5164529453746,
20.3432882291214));
#180870=CARTESIAN_POINT('Ctrl Pts',(20.7762954152734,-19.5094683014143,
20.3428550043192));
#180871=CARTESIAN_POINT('Ctrl Pts',(20.7866465547068,-19.471029450789,20.3404848093727));
#180872=CARTESIAN_POINT('Ctrl Pts',(20.7943880307124,-19.4393919109625,
20.3385853481042));
#180873=CARTESIAN_POINT('Ctrl Pts',(20.8364006996118,-19.2487434345245,
20.3273767205319));
#180874=CARTESIAN_POINT('Ctrl Pts',(20.8529854693216,-19.0863792388588,
20.3187794064944));
#180875=CARTESIAN_POINT('Ctrl Pts',(20.8492492329854,-18.8068802901938,
20.3034769057816));
#180876=CARTESIAN_POINT('Ctrl Pts',(20.8380201086876,-18.690402658304,20.2969546328247));
#180877=CARTESIAN_POINT('Ctrl Pts',(20.8147015410847,-18.5613924012989,
20.2892743167573));
#180878=CARTESIAN_POINT('Ctrl Pts',(20.8120175788886,-18.547356791536,20.2884328134288));
#180879=CARTESIAN_POINT('Ctrl Pts',(20.8075198216203,-18.5250620303588,
20.2870862436861));
#180880=CARTESIAN_POINT('Ctrl Pts',(20.8057982531811,-18.5167845642371,
20.2865841185034));
#180881=CARTESIAN_POINT('Ctrl Pts',(20.8026745699976,-18.5022042542989,
20.2856957174239));
#180882=CARTESIAN_POINT('Ctrl Pts',(20.8012931087123,-18.4958970613438,
20.2853101075588));
#180883=CARTESIAN_POINT('Ctrl Pts',(20.7983761272525,-18.4828648506809,
20.2845106046769));
#180884=CARTESIAN_POINT('Ctrl Pts',(20.7968365495482,-18.4761408284032,
20.284096585308));
#180885=CARTESIAN_POINT('Ctrl Pts',(20.7928002841325,-18.4589003978175,
20.2830310946563));
#180886=CARTESIAN_POINT('Ctrl Pts',(20.790255891726,-18.4483954641057,20.2823780939087));
#180887=CARTESIAN_POINT('Ctrl Pts',(20.7793002217544,-18.4046308838208,
20.2796415419497));
#180888=CARTESIAN_POINT('Ctrl Pts',(20.7701619251216,-18.3715602143114,
20.2775346483525));
#180889=CARTESIAN_POINT('Ctrl Pts',(20.7442601975305,-18.2859820621578,
20.2719769907113));
#180890=CARTESIAN_POINT('Ctrl Pts',(20.7262435650024,-18.2338839147211,
20.2684877854883));
#180891=CARTESIAN_POINT('Ctrl Pts',(20.6664543640362,-18.0806349347482,
20.2579141905084));
#180892=CARTESIAN_POINT('Ctrl Pts',(20.6188548690702,-17.9819610303114,
20.2506814214578));
#180893=CARTESIAN_POINT('Ctrl Pts',(20.5395005856195,-17.8455638043169,
20.2402574808709));
#180894=CARTESIAN_POINT('Ctrl Pts',(20.5137225298926,-17.8045587714529,
20.2370653629312));
#180895=CARTESIAN_POINT('Ctrl Pts',(20.4766378279767,-17.7498289203209,
20.2327524276101));
#180896=CARTESIAN_POINT('Ctrl Pts',(20.4665318091789,-17.7353096289295,
20.2316030570057));
#180897=CARTESIAN_POINT('Ctrl Pts',(20.4252240664983,-17.6775213820953,
20.227012174627));
#180898=CARTESIAN_POINT('Ctrl Pts',(20.3925711674896,-17.6353081949318,
20.223621104637));
#180899=CARTESIAN_POINT('Ctrl Pts',(20.3527634222104,-17.5876796496449,
20.21979193505));
#180900=CARTESIAN_POINT('Ctrl Pts',(20.3471300078977,-17.5810234797385,
20.2192567388969));
#180901=CARTESIAN_POINT('Ctrl Pts',(20.3385382349731,-17.5709981352117,
20.2184507974542));
#180902=CARTESIAN_POINT('Ctrl Pts',(20.3356101161446,-17.5676033318597,
20.2181779153833));
#180903=CARTESIAN_POINT('Ctrl Pts',(20.3303349298428,-17.5615265219983,
20.2176895381327));
#180904=CARTESIAN_POINT('Ctrl Pts',(20.3279918646178,-17.5588411298857,
20.2174737548424));
#180905=CARTESIAN_POINT('Ctrl Pts',(20.3228860372971,-17.5530190740532,
20.2170060061097));
#180906=CARTESIAN_POINT('Ctrl Pts',(20.3201207727011,-17.5498846817113,
20.2167542316922));
#180907=CARTESIAN_POINT('Ctrl Pts',(20.312327717259,-17.5411039101721,20.2160489631704));
#180908=CARTESIAN_POINT('Ctrl Pts',(20.30727887805,-17.5354761791097,20.2155970148345));
#180909=CARTESIAN_POINT('Ctrl Pts',(20.2769252619159,-17.5020047503762,
20.2129085675889));
#180910=CARTESIAN_POINT('Ctrl Pts',(20.2509103215909,-17.4748107576996,
20.2107224536262));
#180911=CARTESIAN_POINT('Ctrl Pts',(20.1629358979216,-17.3876258498124,
20.2036494572595));
#180912=CARTESIAN_POINT('Ctrl Pts',(20.0980329414591,-17.3307224890346,
20.1989257950945));
#180913=CARTESIAN_POINT('Ctrl Pts',(19.8901911631465,-17.1698395991743,
20.1846222364707));
#180914=CARTESIAN_POINT('Ctrl Pts',(19.7375891400057,-17.0796549754226,
20.1751337271928));
#180915=CARTESIAN_POINT('Ctrl Pts',(19.5545458331111,-17.0003549538476,
20.1635411326293));
#180916=CARTESIAN_POINT('Ctrl Pts',(19.533378390977,-16.9915898444035,20.1621988867852));
#180917=CARTESIAN_POINT('Ctrl Pts',(19.5032078544977,-16.9796665720263,
20.1602816776846));
#180918=CARTESIAN_POINT('Ctrl Pts',(19.4943187978461,-16.976222888166,20.1597163252292));
#180919=CARTESIAN_POINT('Ctrl Pts',(19.4798307673967,-16.9707223714449,
20.1587939585398));
#180920=CARTESIAN_POINT('Ctrl Pts',(19.4742457626429,-16.9686289341688,
20.1584381751179));
#180921=CARTESIAN_POINT('Ctrl Pts',(19.4625307855116,-16.9642941630305,
20.1576913997106));
#180922=CARTESIAN_POINT('Ctrl Pts',(19.4563991538341,-16.9620575232385,
20.1573002555702));
#180923=CARTESIAN_POINT('Ctrl Pts',(19.4417768995244,-16.9568002418517,
20.1563667710111));
#180924=CARTESIAN_POINT('Ctrl Pts',(19.4332771908663,-16.95380540967,20.155823579052));
#180925=CARTESIAN_POINT('Ctrl Pts',(19.4045264538029,-16.9438811306457,
20.1539841327016));
#180926=CARTESIAN_POINT('Ctrl Pts',(19.3841900478059,-16.9372047330692,
20.1526795603885));
#180927=CARTESIAN_POINT('Ctrl Pts',(19.2725816986725,-16.9024296476072,
20.145498802058));
#180928=CARTESIAN_POINT('Ctrl Pts',(19.1796014448044,-16.8802268548258,
20.1394325029876));
#180929=CARTESIAN_POINT('Ctrl Pts',(18.9174370425839,-16.8360915784474,
20.1221548578037));
#180930=CARTESIAN_POINT('Ctrl Pts',(18.7466341502385,-16.8281932984175,
20.1106595013735));
#180931=CARTESIAN_POINT('Ctrl Pts',(18.540141983836,-16.8435753205552,20.0974447705595));
#180932=CARTESIAN_POINT('Ctrl Pts',(18.5036223171641,-16.8472524956502,
20.0951366546194));
#180933=CARTESIAN_POINT('Ctrl Pts',(18.4601350065862,-16.8527768363765,
20.092437206709));
#180934=CARTESIAN_POINT('Ctrl Pts',(18.4530601786526,-16.8537119488968,
20.0919996008124));
#180935=CARTESIAN_POINT('Ctrl Pts',(18.4415214171114,-16.855296486326,20.0912885799688));
#180936=CARTESIAN_POINT('Ctrl Pts',(18.4370546583934,-16.8559244262979,
20.0910139979897));
#180937=CARTESIAN_POINT('Ctrl Pts',(18.4290603574544,-16.857074337887,20.0905237950216));
#180938=CARTESIAN_POINT('Ctrl Pts',(18.4255321088041,-16.8575909482428,
20.0903078764517));
#180939=CARTESIAN_POINT('Ctrl Pts',(18.4178913415178,-16.8587294453988,
20.0898412216783));
#180940=CARTESIAN_POINT('Ctrl Pts',(18.4137793581951,-16.8593545355285,
20.0895906690237));
#180941=CARTESIAN_POINT('Ctrl Pts',(18.4022916800185,-16.8611355073814,
20.0888922643463));
#180942=CARTESIAN_POINT('Ctrl Pts',(18.394920134009,-16.8623183055104,20.0884459100984));
#180943=CARTESIAN_POINT('Ctrl Pts',(18.352020930785,-16.8694346594201,20.0858580448895));
#180944=CARTESIAN_POINT('Ctrl Pts',(18.3166407948072,-16.8762355506018,
20.0837626319533));
#180945=CARTESIAN_POINT('Ctrl Pts',(18.2031928520395,-16.9010611719684,
20.0771197047338));
#180946=CARTESIAN_POINT('Ctrl Pts',(18.125965213378,-16.922615362146,20.0727135403215));
#180947=CARTESIAN_POINT('Ctrl Pts',(17.8744490857913,-17.0084658944423,
20.0582255013741));
#180948=CARTESIAN_POINT('Ctrl Pts',(17.7074292920161,-17.0912745602107,
20.0482965085914));
#180949=CARTESIAN_POINT('Ctrl Pts',(17.5350077516949,-17.2071232330054,
20.0362150186401));
#180950=CARTESIAN_POINT('Ctrl Pts',(17.516859682758,-17.2197336413192,20.034919587627));
#180951=CARTESIAN_POINT('Ctrl Pts',(17.4920437698835,-17.2375597841495,
20.0331134233622));
#180952=CARTESIAN_POINT('Ctrl Pts',(17.4852044146602,-17.242535138082,20.0326119152336));
#180953=CARTESIAN_POINT('Ctrl Pts',(17.473501847422,-17.2511559902638,20.0317472901836));
#180954=CARTESIAN_POINT('Ctrl Pts',(17.4686241491818,-17.25478171908,20.0313849438357));
#180955=CARTESIAN_POINT('Ctrl Pts',(17.4587685996162,-17.2621737252347,
20.0306487794923));
#180956=CARTESIAN_POINT('Ctrl Pts',(17.4537916604268,-17.2659411133045,
20.0302749201504));
#180957=CARTESIAN_POINT('Ctrl Pts',(17.4422641877347,-17.2747475169028,
20.029404048733));
#180958=CARTESIAN_POINT('Ctrl Pts',(17.4357263880047,-17.2798029643262,
20.0289063901853));
#180959=CARTESIAN_POINT('Ctrl Pts',(17.422045515538,-17.2905104880988,20.0278570206401));
#180960=CARTESIAN_POINT('Ctrl Pts',(17.4149089987358,-17.2961706326518,
20.0273049933974));
#180961=CARTESIAN_POINT('Ctrl Pts',(17.3960082076488,-17.3113610437656,
20.0258304731548));
#180962=CARTESIAN_POINT('Ctrl Pts',(17.3843094296213,-17.3209716229731,
20.0249047679479));
#180963=CARTESIAN_POINT('Ctrl Pts',(17.3489493617208,-17.3506609641303,
20.0220662692862));
#180964=CARTESIAN_POINT('Ctrl Pts',(17.3256264036911,-17.3711345299148,
20.0201376565915));
#180965=CARTESIAN_POINT('Ctrl Pts',(17.1786303110739,-17.5060072572271,
20.0076107591758));
#180966=CARTESIAN_POINT('Ctrl Pts',(17.0685518872788,-17.6342991144025,
19.9964225465834));
#180967=CARTESIAN_POINT('Ctrl Pts',(16.9197631082974,-17.8565364236068,
19.9788044483057));
#180968=CARTESIAN_POINT('Ctrl Pts',(16.8705046912916,-17.942601249661,19.9723517461347));
#180969=CARTESIAN_POINT('Ctrl Pts',(16.8232353258586,-18.0405388944351,
19.9656327814036));
#180970=CARTESIAN_POINT('Ctrl Pts',(16.8190812886968,-18.0492988732645,
19.9650371083211));
#180971=CARTESIAN_POINT('Ctrl Pts',(16.8130369085061,-18.0622746826635,
19.96416290171));
#180972=CARTESIAN_POINT('Ctrl Pts',(16.8111000205147,-18.0664685160761,
19.9638816023127));
#180973=CARTESIAN_POINT('Ctrl Pts',(16.8076882729552,-18.0739197556727,
19.9633840685189));
#180974=CARTESIAN_POINT('Ctrl Pts',(16.8062079245954,-18.0771745888948,
19.9631674992382));
#180975=CARTESIAN_POINT('Ctrl Pts',(16.8030539889756,-18.0841560105213,
19.962704612285));
#180976=CARTESIAN_POINT('Ctrl Pts',(16.8013829440263,-18.087883686548,19.962458450798));
#180977=CARTESIAN_POINT('Ctrl Pts',(16.7968258157529,-18.0981288236308,
19.9617845621694));
#180978=CARTESIAN_POINT('Ctrl Pts',(16.7939618112104,-18.104656129263,19.9613581669635));
#180979=CARTESIAN_POINT('Ctrl Pts',(16.7788510580554,-18.1395730454917,
19.959092281467));
#180980=CARTESIAN_POINT('Ctrl Pts',(16.7671936907237,-18.1682155204825,
19.9572865138634));
#180981=CARTESIAN_POINT('Ctrl Pts',(16.7525148760944,-18.206674153451,19.9549187101212));
#180982=CARTESIAN_POINT('Ctrl Pts',(16.7489321427425,-18.216269415617,19.9543325979226));
#180983=CARTESIAN_POINT('Ctrl Pts',(16.7454193686617,-18.225889765486,19.9537492327042));
#180984=CARTESIAN_POINT('',(16.6170003908425,-18.9532864008441,20.489056279057));
#180985=CARTESIAN_POINT('Ctrl Pts',(16.7454194015149,-18.2258896755116,
19.7345260518445));
#180986=CARTESIAN_POINT('Ctrl Pts',(16.7805470671853,-18.1296863961113,
19.7401268841278));
#180987=CARTESIAN_POINT('Ctrl Pts',(16.8226235259406,-18.0361205379653,
19.7456314811537));
#180988=CARTESIAN_POINT('Ctrl Pts',(16.920754698698,-17.854436923613,19.7569906966531));
#180989=CARTESIAN_POINT('Ctrl Pts',(16.9768430308415,-17.7667158280565,
19.7628328170713));
#180990=CARTESIAN_POINT('Ctrl Pts',(17.0475681359745,-17.672221026253,19.7697495704607));
#180991=CARTESIAN_POINT('Ctrl Pts',(17.0561041186407,-17.6610499425794,
19.7705776622703));
#180992=CARTESIAN_POINT('Ctrl Pts',(17.0699092552613,-17.6433513288339,
19.7719067746021));
#180993=CARTESIAN_POINT('Ctrl Pts',(17.0751071271484,-17.6367685433421,
19.7724049734974));
#180994=CARTESIAN_POINT('Ctrl Pts',(17.0843685900936,-17.6251817146288,
19.7732888173723));
#180995=CARTESIAN_POINT('Ctrl Pts',(17.0884161969959,-17.6201649888904,
19.7736738183237));
#180996=CARTESIAN_POINT('Ctrl Pts',(17.0968603404038,-17.6097963242568,
19.7744744269932));
#180997=CARTESIAN_POINT('Ctrl Pts',(17.1012603511473,-17.6044473258933,
19.7748901727685));
#180998=CARTESIAN_POINT('Ctrl Pts',(17.1126754381001,-17.590708235081,19.7759651477101));
#180999=CARTESIAN_POINT('Ctrl Pts',(17.1197293573079,-17.5823508152199,
19.7766259591332));
#181000=CARTESIAN_POINT('Ctrl Pts',(17.1499117127893,-17.5471480912477,
19.7794391942736));
#181001=CARTESIAN_POINT('Ctrl Pts',(17.1736463807451,-17.5208323187453,
19.781616626741));
#181002=CARTESIAN_POINT('Ctrl Pts',(17.2376864166998,-17.4533154235877,
19.78740633834));
#181003=CARTESIAN_POINT('Ctrl Pts',(17.2790311894566,-17.4131450266149,
19.7910611796364));
#181004=CARTESIAN_POINT('Ctrl Pts',(17.4217679760684,-17.2853622516311,
19.8033999111042));
#181005=CARTESIAN_POINT('Ctrl Pts',(17.5298269232643,-17.2056906492849,
19.8123263219024));
#181006=CARTESIAN_POINT('Ctrl Pts',(17.7216270372015,-17.0905908270338,
19.8270271227065));
#181007=CARTESIAN_POINT('Ctrl Pts',(17.8014472459869,-17.0493459978098,
19.8328476519824));
#181008=CARTESIAN_POINT('Ctrl Pts',(17.8924920046086,-17.0094124344906,
19.8389896548687));
#181009=CARTESIAN_POINT('Ctrl Pts',(17.9013574933049,-17.0055959771613,
19.8395826563883));
#181010=CARTESIAN_POINT('Ctrl Pts',(17.9144966605783,-17.0000459690647,
19.8404537047473));
#181011=CARTESIAN_POINT('Ctrl Pts',(17.9187502547813,-16.9982655973604,
19.8407344892869));
#181012=CARTESIAN_POINT('Ctrl Pts',(17.92631175527,-16.995129672559,19.8412314547815));
#181013=CARTESIAN_POINT('Ctrl Pts',(17.9296173078232,-16.9937685876548,
19.8414479677669));
#181014=CARTESIAN_POINT('Ctrl Pts',(17.9367125496775,-16.9908680685971,
19.8419111136574));
#181015=CARTESIAN_POINT('Ctrl Pts',(17.9405032468212,-16.989331246961,19.8421575883929));
#181016=CARTESIAN_POINT('Ctrl Pts',(17.9509339837396,-16.985137584304,19.8428332177713));
#181017=CARTESIAN_POINT('Ctrl Pts',(17.9575831404241,-16.9825033608588,
19.8432610289936));
#181018=CARTESIAN_POINT('Ctrl Pts',(17.9933579520465,-16.9685396382364,
19.8455480551594));
#181019=CARTESIAN_POINT('Ctrl Pts',(18.0227200873404,-16.9578217808749,
19.8473727975963));
#181020=CARTESIAN_POINT('Ctrl Pts',(18.2073708560607,-16.8950177611634,
19.8585872796774));
#181021=CARTESIAN_POINT('Ctrl Pts',(18.3680441283967,-16.8604448809359,
19.867242164921));
#181022=CARTESIAN_POINT('Ctrl Pts',(18.6477495083044,-16.8335146082774,
19.8826236740673));
#181023=CARTESIAN_POINT('Ctrl Pts',(18.7651027488652,-16.8319889558617,
19.8891640363662));
#181024=CARTESIAN_POINT('Ctrl Pts',(18.8962303217916,-16.8411767829979,
19.8968647178187));
#181025=CARTESIAN_POINT('Ctrl Pts',(18.9104790372967,-16.8423202932162,
19.8977064888719));
#181026=CARTESIAN_POINT('Ctrl Pts',(18.933136461051,-16.84436977291,19.8990534110273));
#181027=CARTESIAN_POINT('Ctrl Pts',(18.9415533623288,-16.8451819957849,
19.8995556185606));
#181028=CARTESIAN_POINT('Ctrl Pts',(18.9563884359381,-16.8467033280388,
19.9004441205013));
#181029=CARTESIAN_POINT('Ctrl Pts',(18.9628086892343,-16.8473914198324,
19.9008297484497));
#181030=CARTESIAN_POINT('Ctrl Pts',(18.9760805738049,-16.8488752834648,
19.9016292448346));
#181031=CARTESIAN_POINT('Ctrl Pts',(18.9829316571276,-16.8496751902137,
19.9020432394084));
#181032=CARTESIAN_POINT('Ctrl Pts',(19.0005059946725,-16.8518142140413,
19.9031085736971));
#181033=CARTESIAN_POINT('Ctrl Pts',(19.01122302866,-16.8532019710466,19.9037614419402));
#181034=CARTESIAN_POINT('Ctrl Pts',(19.0558970768893,-16.859334985966,19.9064966534943));
#181035=CARTESIAN_POINT('Ctrl Pts',(19.0897453569516,-16.8648225724381,
19.9086023100447));
#181036=CARTESIAN_POINT('Ctrl Pts',(19.1775688356774,-16.8812591182249,
19.9141559119266));
#181037=CARTESIAN_POINT('Ctrl Pts',(19.2312738298428,-16.8934959241307,
19.9176422276242));
#181038=CARTESIAN_POINT('Ctrl Pts',(19.3900378905899,-16.9362462203215,
19.9282102855123));
#181039=CARTESIAN_POINT('Ctrl Pts',(19.4932690692309,-16.9728193543973,
19.9354404234675));
#181040=CARTESIAN_POINT('Ctrl Pts',(19.6343907574575,-17.035488498096,19.945640463466));
#181041=CARTESIAN_POINT('Ctrl Pts',(19.6749836787234,-17.0550894193858,
19.9486119323262));
#181042=CARTESIAN_POINT('Ctrl Pts',(19.736474907382,-17.0872413962037,19.953145621297));
#181043=CARTESIAN_POINT('Ctrl Pts',(19.757833739142,-17.0988823220274,19.9547265584958));
#181044=CARTESIAN_POINT('Ctrl Pts',(19.7915882865671,-17.1180409113933,
19.9572300303378));
#181045=CARTESIAN_POINT('Ctrl Pts',(19.8041153284032,-17.1253221071828,
19.9581602467062));
#181046=CARTESIAN_POINT('Ctrl Pts',(19.8484743481873,-17.1517182139479,
19.9614557631727));
#181047=CARTESIAN_POINT('Ctrl Pts',(19.8798790953437,-17.1715424555092,
19.9637918498234));
#181048=CARTESIAN_POINT('Ctrl Pts',(19.9167024942233,-17.1961654074032,
19.9665198187964));
#181049=CARTESIAN_POINT('Ctrl Pts',(19.9226366668805,-17.2001771825051,
19.9669590791207));
#181050=CARTESIAN_POINT('Ctrl Pts',(19.9322810788318,-17.2067688190714,
19.9676722425014));
#181051=CARTESIAN_POINT('Ctrl Pts',(19.9360035651826,-17.209330539392,19.9679473241312));
#181052=CARTESIAN_POINT('Ctrl Pts',(19.9426493510208,-17.2139354252945,
19.9684380640906));
#181053=CARTESIAN_POINT('Ctrl Pts',(19.9455757058702,-17.2159740701458,
19.968654022789));
#181054=CARTESIAN_POINT('Ctrl Pts',(19.9518987425389,-17.2204027887527,
19.9691203616557));
#181055=CARTESIAN_POINT('Ctrl Pts',(19.9552935364261,-17.2227954581248,
19.9693705604363));
#181056=CARTESIAN_POINT('Ctrl Pts',(19.9647485856289,-17.2295011619625,
19.9700669807399));
#181057=CARTESIAN_POINT('Ctrl Pts',(19.9707932521212,-17.233836217556,19.970511718235));
#181058=CARTESIAN_POINT('Ctrl Pts',(20.005611422008,-17.2590857356219,19.9730714313171));
#181059=CARTESIAN_POINT('Ctrl Pts',(20.0338788372301,-17.2806922305908,
19.9751414727124));
#181060=CARTESIAN_POINT('Ctrl Pts',(20.1227035916488,-17.3522040719066,
19.9816674583579));
#181061=CARTESIAN_POINT('Ctrl Pts',(20.1810396157034,-17.4047692662367,
19.9859877187922));
#181062=CARTESIAN_POINT('Ctrl Pts',(20.3688979775496,-17.5939856051794,
20.0005313012805));
#181063=CARTESIAN_POINT('Ctrl Pts',(20.4830620021931,-17.7445767773613,
20.0105821242138));
#181064=CARTESIAN_POINT('Ctrl Pts',(20.5865921456588,-17.9272715407187,
20.0227985062851));
#181065=CARTESIAN_POINT('Ctrl Pts',(20.5970657291424,-17.9464394051464,
20.0240791289184));
#181066=CARTESIAN_POINT('Ctrl Pts',(20.6111617514148,-17.9732131976032,
20.0258678733392));
#181067=CARTESIAN_POINT('Ctrl Pts',(20.6150384242497,-17.9806842486053,
20.0263670041261));
#181068=CARTESIAN_POINT('Ctrl Pts',(20.6216325552855,-17.993579870596,20.0272286183272));
#181069=CARTESIAN_POINT('Ctrl Pts',(20.6243714561481,-17.9989934077762,
20.0275903434822));
#181070=CARTESIAN_POINT('Ctrl Pts',(20.6299763470006,-18.0101909114067,
20.0283386268809));
#181071=CARTESIAN_POINT('Ctrl Pts',(20.632839225805,-18.0159763566793,20.0287252891717));
#181072=CARTESIAN_POINT('Ctrl Pts',(20.6394506640489,-18.0294922343711,
20.0296287515117));
#181073=CARTESIAN_POINT('Ctrl Pts',(20.6431786939973,-18.0372325313185,
20.0301462597869));
#181074=CARTESIAN_POINT('Ctrl Pts',(20.6550037767144,-18.0621714531796,
20.0318141325822));
#181075=CARTESIAN_POINT('Ctrl Pts',(20.6629161564608,-18.0794561459516,
20.0329708459852));
#181076=CARTESIAN_POINT('Ctrl Pts',(20.7015120020373,-18.1668607320337,
20.0388253434902));
#181077=CARTESIAN_POINT('Ctrl Pts',(20.728606331535,-18.2384942470877,20.043643404423));
#181078=CARTESIAN_POINT('Ctrl Pts',(20.7850259438845,-18.4162132051225,
20.0556347989979));
#181079=CARTESIAN_POINT('Ctrl Pts',(20.8100759289639,-18.5234207200323,
20.0629064440229));
#181080=CARTESIAN_POINT('Ctrl Pts',(20.8373686026678,-18.7019490180111,
20.0748350385553));
#181081=CARTESIAN_POINT('Ctrl Pts',(20.8445447065821,-18.7723141522826,
20.0794882829132));
#181082=CARTESIAN_POINT('Ctrl Pts',(20.8506425760097,-18.8904915403675,
20.0871064238349));
#181083=CARTESIAN_POINT('Ctrl Pts',(20.8514909562973,-18.9381471566793,
20.090124697644));
#181084=CARTESIAN_POINT('Ctrl Pts',(20.8506069586826,-18.9935165982999,
20.0935390885672));
#181085=CARTESIAN_POINT('Ctrl Pts',(20.8504414148626,-19.0012380655234,
20.094013142129));
#181086=CARTESIAN_POINT('Ctrl Pts',(20.8501088494901,-19.0135941658069,
20.0947681954648));
#181087=CARTESIAN_POINT('Ctrl Pts',(20.8499688502697,-19.0182293725133,
20.0950506449308));
#181088=CARTESIAN_POINT('Ctrl Pts',(20.8496935528338,-19.0264490182648,
20.0955500550927));
#181089=CARTESIAN_POINT('Ctrl Pts',(20.8495643741406,-19.0300336172403,
20.095767354518));
#181090=CARTESIAN_POINT('Ctrl Pts',(20.8492707881097,-19.0376429674077,
20.0962275733651));
#181091=CARTESIAN_POINT('Ctrl Pts',(20.8491040049387,-19.0416675739152,
20.0964703584332));
#181092=CARTESIAN_POINT('Ctrl Pts',(20.8486216767113,-19.0525552852036,
20.0971255264038));
#181093=CARTESIAN_POINT('Ctrl Pts',(20.8482842046051,-19.0594174385846,
20.0975366982362));
#181094=CARTESIAN_POINT('Ctrl Pts',(20.8464248682664,-19.0938114437129,
20.0995892687076));
#181095=CARTESIAN_POINT('Ctrl Pts',(20.8443985385574,-19.1213147432433,
20.1012040233315));
#181096=CARTESIAN_POINT('Ctrl Pts',(20.8369402554542,-19.2012083688462,
20.1058374163366));
#181097=CARTESIAN_POINT('Ctrl Pts',(20.8300898620696,-19.2534474654108,
20.1087953003085));
#181098=CARTESIAN_POINT('Ctrl Pts',(20.7978729314948,-19.4437421511963,
20.1194779234525));
#181099=CARTESIAN_POINT('Ctrl Pts',(20.7607489010224,-19.5794336791868,
20.1269381944543));
#181100=CARTESIAN_POINT('Ctrl Pts',(20.6771589183375,-19.7972615199283,
20.1398370889753));
#181101=CARTESIAN_POINT('Ctrl Pts',(20.6381698851839,-19.8817674888697,
20.1450882757069));
#181102=CARTESIAN_POINT('Ctrl Pts',(20.5871670337418,-19.9755483317184,
20.1513463222675));
#181103=CARTESIAN_POINT('Ctrl Pts',(20.5804591410119,-19.9876002459716,
20.1521589521558));
#181104=CARTESIAN_POINT('Ctrl Pts',(20.5695220576024,-20.006806535564,20.153467908742));
#181105=CARTESIAN_POINT('Ctrl Pts',(20.5653676055214,-20.0140031741268,
20.1539615487339));
#181106=CARTESIAN_POINT('Ctrl Pts',(20.557921528808,-20.0267281759423,20.154840124743));
#181107=CARTESIAN_POINT('Ctrl Pts',(20.5546468518162,-20.0322663722316,
20.1552244421332));
#181108=CARTESIAN_POINT('Ctrl Pts',(20.5477769766532,-20.0437648689254,
20.156026462982));
#181109=CARTESIAN_POINT('Ctrl Pts',(20.5441775314504,-20.0497225300086,
20.1564443185528));
#181110=CARTESIAN_POINT('Ctrl Pts',(20.5347659407548,-20.0651280560199,
20.1575308860973));
#181111=CARTESIAN_POINT('Ctrl Pts',(20.5289088590093,-20.0745480938452,
20.1582012458132));
#181112=CARTESIAN_POINT('Ctrl Pts',(20.5032689013427,-20.1150715061749,
20.1611112162393));
#181113=CARTESIAN_POINT('Ctrl Pts',(20.4827505349386,-20.1456997412839,
20.1633780270702));
#181114=CARTESIAN_POINT('Ctrl Pts',(20.4262468486197,-20.2254586287154,
20.1694666057189));
#181115=CARTESIAN_POINT('Ctrl Pts',(20.388925480486,-20.2735963247478,20.1733366023569));
#181116=CARTESIAN_POINT('Ctrl Pts',(20.2457494232857,-20.4426778973935,
20.1876414227859));
#181117=CARTESIAN_POINT('Ctrl Pts',(20.1283032675158,-20.5530680687911,
20.1984390453116));
#181118=CARTESIAN_POINT('Ctrl Pts',(19.9521815025712,-20.6843995608512,
20.2126879119689));
#181119=CARTESIAN_POINT('Ctrl Pts',(19.9033933730999,-20.7176995507841,
20.2164535629882));
#181120=CARTESIAN_POINT('Ctrl Pts',(19.8456903419437,-20.7536418558616,
20.2206488561441));
#181121=CARTESIAN_POINT('Ctrl Pts',(19.838078254587,-20.7583166963077,20.2211972789703));
#181122=CARTESIAN_POINT('Ctrl Pts',(19.8265626690247,-20.7652888141176,
20.2220191380875));
#181123=CARTESIAN_POINT('Ctrl Pts',(19.8226811269092,-20.7676219083122,
20.2222948364231));
#181124=CARTESIAN_POINT('Ctrl Pts',(19.8157287864319,-20.7717704684062,
20.2227862419451));
#181125=CARTESIAN_POINT('Ctrl Pts',(19.8126608682162,-20.7735906392703,
20.2230022529377));
#181126=CARTESIAN_POINT('Ctrl Pts',(19.8060173208294,-20.7775095323721,
20.2234682121569));
#181127=CARTESIAN_POINT('Ctrl Pts',(19.8024401340686,-20.7796055016136,
20.2237179816327));
#181128=CARTESIAN_POINT('Ctrl Pts',(19.7924566053026,-20.7854157878599,
20.2244119999043));
#181129=CARTESIAN_POINT('Ctrl Pts',(19.7860368255959,-20.7891070621364,
20.2248547812215));
#181130=CARTESIAN_POINT('Ctrl Pts',(19.7491314869355,-20.8100701643897,
20.2273809787281));
#181131=CARTESIAN_POINT('Ctrl Pts',(19.7182383083398,-20.8266178134458,
20.2294208254995));
#181132=CARTESIAN_POINT('Ctrl Pts',(19.6186103344541,-20.8768402762856,
20.2358094510425));
#181133=CARTESIAN_POINT('Ctrl Pts',(19.5484508390511,-20.9075605787205,
20.2400290466047));
#181134=CARTESIAN_POINT('Ctrl Pts',(19.2977415968042,-21.00149700293,20.2546427344995));
#181135=CARTESIAN_POINT('Ctrl Pts',(19.1104657182348,-21.0440111564456,
20.2648395706612));
#181136=CARTESIAN_POINT('Ctrl Pts',(18.8986139739447,-21.0626997512307,
20.2772165061168));
#181137=CARTESIAN_POINT('Ctrl Pts',(18.8771713707648,-21.0642625567977,
20.2784773115034));
#181138=CARTESIAN_POINT('Ctrl Pts',(18.8473618295938,-21.0659791877052,
20.2802426699385));
#181139=CARTESIAN_POINT('Ctrl Pts',(18.8390117297827,-21.0664104246855,
20.2807385402028));
#181140=CARTESIAN_POINT('Ctrl Pts',(18.8246133213678,-21.0670685230588,
20.2815960291988));
#181141=CARTESIAN_POINT('Ctrl Pts',(18.8185661500767,-21.0673189348971,
20.2819569064628));
#181142=CARTESIAN_POINT('Ctrl Pts',(18.8060591709852,-21.0677831293116,
20.2827048536851));
#181143=CARTESIAN_POINT('Ctrl Pts',(18.7995992984212,-21.0679932667691,
20.2830920339934));
#181144=CARTESIAN_POINT('Ctrl Pts',(18.7844986935655,-21.0684152684608,
20.28399917092));
#181145=CARTESIAN_POINT('Ctrl Pts',(18.7758574716495,-21.0686038021395,
20.2845198532456));
#181146=CARTESIAN_POINT('Ctrl Pts',(18.7479225577069,-21.069042151022,20.2862083194631));
#181147=CARTESIAN_POINT('Ctrl Pts',(18.7286269651951,-21.0690811034595,
20.2873826739654));
#181148=CARTESIAN_POINT('Ctrl Pts',(18.6306517019469,-21.06793947872,20.2933882035967));
#181149=CARTESIAN_POINT('Ctrl Pts',(18.5520906242898,-21.0626366974371,
20.2983467403219));
#181150=CARTESIAN_POINT('Ctrl Pts',(18.3720042015798,-21.040351840264,20.3100318878856));
#181151=CARTESIAN_POINT('Ctrl Pts',(18.271055601448,-21.0203167156928,20.3168231199227));
#181152=CARTESIAN_POINT('Ctrl Pts',(18.0548301710431,-20.9607755953748,
20.3316409160328));
#181153=CARTESIAN_POINT('Ctrl Pts',(17.9406711823433,-20.9184910992178,
20.3396418470578));
#181154=CARTESIAN_POINT('Ctrl Pts',(17.8221907809327,-20.8625974806489,
20.3477326435652));
#181155=CARTESIAN_POINT('Ctrl Pts',(17.8136480826569,-20.8584970865319,
20.3483146849025));
#181156=CARTESIAN_POINT('Ctrl Pts',(17.801020453579,-20.8523313162533,20.3491727597964));
#181157=CARTESIAN_POINT('Ctrl Pts',(17.7969143617505,-20.8503098938446,
20.349451416912));
#181158=CARTESIAN_POINT('Ctrl Pts',(17.789615757918,-20.8466873510864,20.3499460449661));
#181159=CARTESIAN_POINT('Ctrl Pts',(17.7864207174449,-20.8450914555257,
20.3501623361305));
#181160=CARTESIAN_POINT('Ctrl Pts',(17.7796287575105,-20.841677425954,20.350621609908));
#181161=CARTESIAN_POINT('Ctrl Pts',(17.7760329990429,-20.8398571101519,
20.3508644529268));
#181162=CARTESIAN_POINT('Ctrl Pts',(17.7662297297349,-20.8348590850703,
20.3515257573096));
#181163=CARTESIAN_POINT('Ctrl Pts',(17.7600326231549,-20.8316609221254,
20.3519429545262));
#181164=CARTESIAN_POINT('Ctrl Pts',(17.7462223590738,-20.8244471723838,
20.3528710401299));
#181165=CARTESIAN_POINT('Ctrl Pts',(17.7386176166978,-20.8204156383723,
20.3533809781286));
#181166=CARTESIAN_POINT('Ctrl Pts',(17.7152720038246,-20.8078563404309,
20.3549436150115));
#181167=CARTESIAN_POINT('Ctrl Pts',(17.6996141548693,-20.799174992557,20.3559877143731));
#181168=CARTESIAN_POINT('Ctrl Pts',(17.6398791393012,-20.7650576773131,
20.3599629557947));
#181169=CARTESIAN_POINT('Ctrl Pts',(17.5966117920201,-20.738232727672,20.3628255060107));
#181170=CARTESIAN_POINT('Ctrl Pts',(17.4424243266523,-20.6347626986873,
20.3731182866498));
#181171=CARTESIAN_POINT('Ctrl Pts',(17.3379252307763,-20.5491335902069,
20.3802936736151));
#181172=CARTESIAN_POINT('Ctrl Pts',(17.1708493965805,-20.3832169122454,
20.3932651296098));
#181173=CARTESIAN_POINT('Ctrl Pts',(17.1045822428723,-20.3072917346343,
20.3989293074954));
#181174=CARTESIAN_POINT('Ctrl Pts',(17.035548290577,-20.215782571959,20.4056473067735));
#181175=CARTESIAN_POINT('Ctrl Pts',(17.0272365379278,-20.2045346577935,
20.406471141151));
#181176=CARTESIAN_POINT('Ctrl Pts',(17.014131840751,-20.1864280086187,20.4077947087111));
#181177=CARTESIAN_POINT('Ctrl Pts',(17.0092669658064,-20.1796216645841,
20.4082916577737));
#181178=CARTESIAN_POINT('Ctrl Pts',(17.0007273822617,-20.167523155208,20.4091740573063));
#181179=CARTESIAN_POINT('Ctrl Pts',(16.9970362280716,-20.1622426871665,
20.4095588707449));
#181180=CARTESIAN_POINT('Ctrl Pts',(16.9894217324656,-20.1512429987109,
20.4103598600947));
#181181=CARTESIAN_POINT('Ctrl Pts',(16.9855022822326,-20.1455211898797,
20.4107761778783));
#181182=CARTESIAN_POINT('Ctrl Pts',(16.975451360508,-20.1306925852483,20.4118542857492));
#181183=CARTESIAN_POINT('Ctrl Pts',(16.9693625437384,-20.1215572533339,
20.4125176756502));
#181184=CARTESIAN_POINT('Ctrl Pts',(16.9437147949679,-20.0824205030374,
20.4153566730717));
#181185=CARTESIAN_POINT('Ctrl Pts',(16.9248487405476,-20.0519741376835,
20.4175578628909));
#181186=CARTESIAN_POINT('Ctrl Pts',(16.8772303561213,-19.9705852968379,
20.4234264701927));
#181187=CARTESIAN_POINT('Ctrl Pts',(16.8498027401428,-19.9189070450648,
20.4271379056861));
#181188=CARTESIAN_POINT('Ctrl Pts',(16.7582330083887,-19.7276417390236,
20.4408045120723));
#181189=CARTESIAN_POINT('Ctrl Pts',(16.7071876152669,-19.5823176408604,
20.4510983065187));
#181190=CARTESIAN_POINT('Ctrl Pts',(16.6660226855411,-19.4057911702342,
20.4629186754329));
#181191=CARTESIAN_POINT('Ctrl Pts',(16.6602607812044,-19.3786876543303,
20.4647138057823));
#181192=CARTESIAN_POINT('Ctrl Pts',(16.6468711367126,-19.3090051237982,
20.4692668120853));
#181193=CARTESIAN_POINT('Ctrl Pts',(16.6400127084185,-19.2662886606018,
20.4719989723584));
#181194=CARTESIAN_POINT('Ctrl Pts',(16.6335056830334,-19.215948681038,20.4751271739653));
#181195=CARTESIAN_POINT('Ctrl Pts',(16.6325834880109,-19.208503272498,20.4755875014242));
#181196=CARTESIAN_POINT('Ctrl Pts',(16.6311572014448,-19.1964637424467,
20.4763279164765));
#181197=CARTESIAN_POINT('Ctrl Pts',(16.6306285495896,-19.1918726731822,
20.4766093334647));
#181198=CARTESIAN_POINT('Ctrl Pts',(16.6297175168666,-19.1837261699198,
20.4771069971511));
#181199=CARTESIAN_POINT('Ctrl Pts',(16.6293291064758,-19.180171464651,20.4773235793922));
#181200=CARTESIAN_POINT('Ctrl Pts',(16.6285936556603,-19.1732789772606,
20.4777424096378));
#181201=CARTESIAN_POINT('Ctrl Pts',(16.6282455464994,-19.1699413739676,
20.4779447190852));
#181202=CARTESIAN_POINT('Ctrl Pts',(16.627496289301,-19.162588228519,20.4783893491729));
#181203=CARTESIAN_POINT('Ctrl Pts',(16.6270986830808,-19.1585723276542,
20.4786314723414));
#181204=CARTESIAN_POINT('Ctrl Pts',(16.6261439843523,-19.1486401023826,
20.4792285954265));
#181205=CARTESIAN_POINT('Ctrl Pts',(16.625600310828,-19.142722481973,20.4795828693057));
#181206=CARTESIAN_POINT('Ctrl Pts',(16.6234160992151,-19.1177968324816,
20.481069122359));
#181207=CARTESIAN_POINT('Ctrl Pts',(16.6220075783014,-19.0987687221853,
20.4821890723319));
#181208=CARTESIAN_POINT('Ctrl Pts',(16.6183136910291,-19.0376545455932,
20.4857465427669));
#181209=CARTESIAN_POINT('Ctrl Pts',(16.6170276587043,-18.9955169040541,
20.4881393462053));
#181210=CARTESIAN_POINT('Ctrl Pts',(16.6170004413562,-18.953367004782,20.4904971916622));
#181211=CARTESIAN_POINT('Ctrl Pts',(16.7454193692319,-18.2258897639242,
20.5336910470276));
#181212=CARTESIAN_POINT('Ctrl Pts',(16.7207024917391,-18.2935812815386,
20.529371954925));
#181213=CARTESIAN_POINT('Ctrl Pts',(16.6994546610031,-18.3625126961517,
20.5250528628225));
#181214=CARTESIAN_POINT('Ctrl Pts',(16.6817841805163,-18.4322892821379,
20.5207337707199));
#181215=CARTESIAN_POINT('Ctrl Pts',(16.6641059734603,-18.5020963785351,
20.5164127900573));
#181216=CARTESIAN_POINT('Ctrl Pts',(16.6500083270565,-18.572748895104,20.5120918093947));
#181217=CARTESIAN_POINT('Ctrl Pts',(16.6395483122343,-18.643842365638,20.5077708287321));
#181218=CARTESIAN_POINT('Ctrl Pts',(16.629072807401,-18.7150411169649,20.503443449222));
#181219=CARTESIAN_POINT('Ctrl Pts',(16.6222457295304,-18.7866816316723,
20.499116069712));
#181220=CARTESIAN_POINT('Ctrl Pts',(16.6190721599129,-18.8583558265323,
20.4947886902019));
#181221=CARTESIAN_POINT('Ctrl Pts',(16.6176708340988,-18.8900043836992,
20.492877886487));
#181222=CARTESIAN_POINT('Ctrl Pts',(16.6169811726838,-18.9216595290166,
20.490967082772));
#181223=CARTESIAN_POINT('Ctrl Pts',(16.6170003908425,-18.9532864008441,
20.489056279057));
#181224=CARTESIAN_POINT('Origin',(18.734,-18.952,0.));
#181225=CARTESIAN_POINT('',(16.7454193692319,-18.2258897639242,21.5555703664997));
#181226=CARTESIAN_POINT('',(16.7454193692319,-18.2258897639242,21.3335535355786));
#181227=CARTESIAN_POINT('',(16.7454193692319,-18.2258897639242,0.));
#181228=CARTESIAN_POINT('',(16.6170006158577,-18.953614788214,21.5109437210328));
#181229=CARTESIAN_POINT('Ctrl Pts',(16.6170006158577,-18.953614788214,21.5109437210328));
#181230=CARTESIAN_POINT('Ctrl Pts',(16.6169459675925,-18.8819705053332,
21.515267181378));
#181231=CARTESIAN_POINT('Ctrl Pts',(16.6205324541972,-18.8101917050093,
21.5195906417233));
#181232=CARTESIAN_POINT('Ctrl Pts',(16.6277745368492,-18.7386849785526,
21.5239141020685));
#181233=CARTESIAN_POINT('Ctrl Pts',(16.6350090210574,-18.6672532774524,
21.5282330262089));
#181234=CARTESIAN_POINT('Ctrl Pts',(16.6458914496557,-18.5960935752594,
21.5325519503494));
#181235=CARTESIAN_POINT('Ctrl Pts',(16.6603842616694,-18.5256119493375,
21.5368708744898));
#181236=CARTESIAN_POINT('Ctrl Pts',(16.6748666465897,-18.4551810325882,
21.5411866913088));
#181237=CARTESIAN_POINT('Ctrl Pts',(16.6929541629953,-18.3854277094975,
21.5455025081278));
#181238=CARTESIAN_POINT('Ctrl Pts',(16.7145577235254,-18.3167505277555,
21.5498183249468));
#181239=CARTESIAN_POINT('Ctrl Pts',(16.7241553333615,-18.2862399647356,
21.5517356721311));
#181240=CARTESIAN_POINT('Ctrl Pts',(16.7344462197403,-18.2559416643843,
21.5536530193154));
#181241=CARTESIAN_POINT('Ctrl Pts',(16.7454193692319,-18.2258897639242,
21.5555703664997));
#181242=CARTESIAN_POINT('Ctrl Pts',(16.6170005689161,-18.9535520277953,
21.5099894676285));
#181243=CARTESIAN_POINT('Ctrl Pts',(16.6170514757345,-19.0229900275103,
21.5054225881129));
#181244=CARTESIAN_POINT('Ctrl Pts',(16.620518744223,-19.0923904496927,21.5009009048524));
#181245=CARTESIAN_POINT('Ctrl Pts',(16.6297026110579,-19.1847375792016,
21.4950376377229));
#181246=CARTESIAN_POINT('Ctrl Pts',(16.6323978968568,-19.2079355069445,
21.4935779411454));
#181247=CARTESIAN_POINT('Ctrl Pts',(16.6362853529812,-19.2371664355986,
21.4917592136074));
#181248=CARTESIAN_POINT('Ctrl Pts',(16.6371205542672,-19.2432442762527,
21.491382182899));
#181249=CARTESIAN_POINT('Ctrl Pts',(16.6385604120732,-19.2533948985387,
21.4907544855754));
#181250=CARTESIAN_POINT('Ctrl Pts',(16.6391505446227,-19.2574696572047,
21.4905030441404));
#181251=CARTESIAN_POINT('Ctrl Pts',(16.6402462872948,-19.2648830325642,
21.4900465921496));
#181252=CARTESIAN_POINT('Ctrl Pts',(16.6407480030291,-19.2682221989029,
21.4898413667541));
#181253=CARTESIAN_POINT('Ctrl Pts',(16.6417946456342,-19.2750764736125,
21.4894208862801));
#181254=CARTESIAN_POINT('Ctrl Pts',(16.64234044042,-19.2785913960278,21.489205687508));
#181255=CARTESIAN_POINT('Ctrl Pts',(16.6435933949801,-19.286528444324,21.4887207108561));
#181256=CARTESIAN_POINT('Ctrl Pts',(16.6443057263194,-19.2909496979963,
21.4884512303207));
#181257=CARTESIAN_POINT('Ctrl Pts',(16.6465011846869,-19.3043063085817,
21.4876390674743));
#181258=CARTESIAN_POINT('Ctrl Pts',(16.6480276539481,-19.3132345736134,
21.4870987991144));
#181259=CARTESIAN_POINT('Ctrl Pts',(16.6601842244475,-19.3816901054389,
21.4829746672044));
#181260=CARTESIAN_POINT('Ctrl Pts',(16.6733041426196,-19.4407529849975,
21.4795222754193));
#181261=CARTESIAN_POINT('Ctrl Pts',(16.6938224022332,-19.5174393922494,
21.4750845544611));
#181262=CARTESIAN_POINT('Ctrl Pts',(16.6989527891217,-19.5356344855662,
21.4740350315778));
#181263=CARTESIAN_POINT('Ctrl Pts',(16.7159624561297,-19.5930064378668,
21.4707298068458));
#181264=CARTESIAN_POINT('Ctrl Pts',(16.7287348634327,-19.6319093108685,
21.4684945478098));
#181265=CARTESIAN_POINT('Ctrl Pts',(16.7545785188735,-19.7035449482025,
21.4643518492426));
#181266=CARTESIAN_POINT('Ctrl Pts',(16.7673542878302,-19.7363684517502,
21.4624429450972));
#181267=CARTESIAN_POINT('Ctrl Pts',(16.8090252811438,-19.8360012189636,
21.4565793344634));
#181268=CARTESIAN_POINT('Ctrl Pts',(16.8405504665062,-19.9016494246912,
21.452616563004));
#181269=CARTESIAN_POINT('Ctrl Pts',(16.9018314006153,-20.0140248950145,
21.445503598111));
#181270=CARTESIAN_POINT('Ctrl Pts',(16.9301557787408,-20.0614521294023,
21.4423912249842));
#181271=CARTESIAN_POINT('Ctrl Pts',(16.9790291445708,-20.1364590544566,
21.437242443796));
#181272=CARTESIAN_POINT('Ctrl Pts',(16.9984530235103,-20.1647417077771,
21.4352459079915));
#181273=CARTESIAN_POINT('Ctrl Pts',(17.0248611085902,-20.2012594082697,
21.4325885617402));
#181274=CARTESIAN_POINT('Ctrl Pts',(17.0312338007241,-20.2099316688001,
21.4319514451171));
#181275=CARTESIAN_POINT('Ctrl Pts',(17.0417740979783,-20.2240485456339,
21.4309042020825));
#181276=CARTESIAN_POINT('Ctrl Pts',(17.0459025703592,-20.2295222394353,
21.4304956168755));
#181277=CARTESIAN_POINT('Ctrl Pts',(17.0539413835458,-20.2400734125033,
21.4297030690238));
#181278=CARTESIAN_POINT('Ctrl Pts',(17.0578483390271,-20.2451533856151,
21.4293192434305));
#181279=CARTESIAN_POINT('Ctrl Pts',(17.0669162730086,-20.2568337239774,
21.4284314759975));
#181280=CARTESIAN_POINT('Ctrl Pts',(17.0720934640131,-20.26342131388,21.427926888305));
#181281=CARTESIAN_POINT('Ctrl Pts',(17.0861067224784,-20.2810358966646,
21.4265670572115));
#181282=CARTESIAN_POINT('Ctrl Pts',(17.095014197555,-20.2920052958124,21.425708937557));
#181283=CARTESIAN_POINT('Ctrl Pts',(17.1997104957267,-20.4183312382032,
21.4156928955381));
#181284=CARTESIAN_POINT('Ctrl Pts',(17.30736564342,-20.5232638048164,21.4060185095525));
#181285=CARTESIAN_POINT('Ctrl Pts',(17.4998886808629,-20.6746996138827,
21.3898623194387));
#181286=CARTESIAN_POINT('Ctrl Pts',(17.5784756438701,-20.728369537953,21.3835372013986));
#181287=CARTESIAN_POINT('Ctrl Pts',(17.6991998501707,-20.7994046229204,
21.3744154243431));
#181288=CARTESIAN_POINT('Ctrl Pts',(17.7387161832013,-20.8209905935789,
21.3715175782669));
#181289=CARTESIAN_POINT('Ctrl Pts',(17.8009151235537,-20.8524342986676,
21.367122344912));
#181290=CARTESIAN_POINT('Ctrl Pts',(17.8231312489496,-20.8631818732465,
21.3655841969589));
#181291=CARTESIAN_POINT('Ctrl Pts',(17.8514873236358,-20.876292969929,21.3636654975228));
#181292=CARTESIAN_POINT('Ctrl Pts',(17.8574561994436,-20.8790192075851,
21.3632640852257));
#181293=CARTESIAN_POINT('Ctrl Pts',(17.8664998554624,-20.8830991129605,
21.3626597245716));
#181294=CARTESIAN_POINT('Ctrl Pts',(17.8695652741808,-20.8844732572568,
21.3624555348102));
#181295=CARTESIAN_POINT('Ctrl Pts',(17.8758768732228,-20.8872845532612,
21.362036496942));
#181296=CARTESIAN_POINT('Ctrl Pts',(17.8791233500479,-20.8887208152752,
21.3618217113365));
#181297=CARTESIAN_POINT('Ctrl Pts',(17.8864142923672,-20.8919244698704,
21.3613410118763));
#181298=CARTESIAN_POINT('Ctrl Pts',(17.8904606766289,-20.8936873824908,
21.3610753741924));
#181299=CARTESIAN_POINT('Ctrl Pts',(17.9007719012331,-20.8981414195365,
21.3604012976051));
#181300=CARTESIAN_POINT('Ctrl Pts',(17.9070443375919,-20.9008149795909,
21.3599939052019));
#181301=CARTESIAN_POINT('Ctrl Pts',(17.9427393211832,-20.9158262225968,
21.3576899849652));
#181302=CARTESIAN_POINT('Ctrl Pts',(17.9724265960238,-20.9275285599298,
21.3558294339172));
#181303=CARTESIAN_POINT('Ctrl Pts',(18.1885432690977,-21.0071224391009,
21.3426052568029));
#181304=CARTESIAN_POINT('Ctrl Pts',(18.3834490244943,-21.0491849386751,
21.3322947224257));
#181305=CARTESIAN_POINT('Ctrl Pts',(18.6371247253503,-21.0675206933882,
21.3181606462519));
#181306=CARTESIAN_POINT('Ctrl Pts',(18.6930029352775,-21.0693405949616,
21.3150107969211));
#181307=CARTESIAN_POINT('Ctrl Pts',(18.7835680454164,-21.0687038019494,
21.309801662039));
#181308=CARTESIAN_POINT('Ctrl Pts',(18.8182383208852,-21.0676076382361,
21.307782974275));
#181309=CARTESIAN_POINT('Ctrl Pts',(18.8637161113335,-21.0650501312871,
21.3050967260059));
#181310=CARTESIAN_POINT('Ctrl Pts',(18.8745625673642,-21.0643563347299,
21.3044532004413));
#181311=CARTESIAN_POINT('Ctrl Pts',(18.8923078656794,-21.063083973047,21.303395506849));
#181312=CARTESIAN_POINT('Ctrl Pts',(18.8992101478068,-21.0625550281638,
21.3029828981763));
#181313=CARTESIAN_POINT('Ctrl Pts',(18.9125583738092,-21.0614662286663,
21.3021825812569));
#181314=CARTESIAN_POINT('Ctrl Pts',(18.9190045968349,-21.0609106572951,
21.3017950117789));
#181315=CARTESIAN_POINT('Ctrl Pts',(18.9338721230383,-21.0595606001864,
21.300898600921));
#181316=CARTESIAN_POINT('Ctrl Pts',(18.942291371816,-21.058745179232,21.3003891073578));
#181317=CARTESIAN_POINT('Ctrl Pts',(18.9648977846113,-21.0564188673869,
21.2990159480839));
#181318=CARTESIAN_POINT('Ctrl Pts',(18.9790747481408,-21.0548149962795,
21.2981493777601));
#181319=CARTESIAN_POINT('Ctrl Pts',(19.1068139128671,-21.0390542716253,
21.2902909847284));
#181320=CARTESIAN_POINT('Ctrl Pts',(19.2190520317045,-21.0158563304589,
21.2830111545704));
#181321=CARTESIAN_POINT('Ctrl Pts',(19.4859266474189,-20.9377197327291,
21.2648703778687));
#181322=CARTESIAN_POINT('Ctrl Pts',(19.637133800448,-20.8736725972321,21.2538528597599));
#181323=CARTESIAN_POINT('Ctrl Pts',(19.8079481029028,-20.7766639129949,
21.2413707544212));
#181324=CARTESIAN_POINT('Ctrl Pts',(19.8360663236225,-20.7598199618748,
21.2393167900982));
#181325=CARTESIAN_POINT('Ctrl Pts',(19.8699385060303,-20.7384449825376,
21.2368539161157));
#181326=CARTESIAN_POINT('Ctrl Pts',(19.8760732407335,-20.7345292932913,
21.2364083234476));
#181327=CARTESIAN_POINT('Ctrl Pts',(19.8856564238649,-20.7283427392234,
21.2357131445788));
#181328=CARTESIAN_POINT('Ctrl Pts',(19.8891185620725,-20.726093332958,21.2354621790488));
#181329=CARTESIAN_POINT('Ctrl Pts',(19.8955710570241,-20.7218741484199,
21.2349948231166));
#181330=CARTESIAN_POINT('Ctrl Pts',(19.8985629708215,-20.7199069288454,
21.2347782737317));
#181331=CARTESIAN_POINT('Ctrl Pts',(19.9053761830702,-20.7154023583099,
21.2342854893252));
#181332=CARTESIAN_POINT('Ctrl Pts',(19.9091942256614,-20.7128601796951,
21.2340095821272));
#181333=CARTESIAN_POINT('Ctrl Pts',(19.9209015364339,-20.7050100275109,
21.233164215217));
#181334=CARTESIAN_POINT('Ctrl Pts',(19.9287634550979,-20.6996612107963,
21.2325974300523));
#181335=CARTESIAN_POINT('Ctrl Pts',(19.9989616830963,-20.6512071007596,
21.2275423215691));
#181336=CARTESIAN_POINT('Ctrl Pts',(20.0589845694252,-20.6048313017748,
21.2232594657571));
#181337=CARTESIAN_POINT('Ctrl Pts',(20.2235750656522,-20.4629209023133,
21.2112292821058));
#181338=CARTESIAN_POINT('Ctrl Pts',(20.3212188237948,-20.35999665412,21.2037067473853));
#181339=CARTESIAN_POINT('Ctrl Pts',(20.4457144141763,-20.1992148075485,
21.1924562677934));
#181340=CARTESIAN_POINT('Ctrl Pts',(20.4814022607839,-20.1487019229487,
21.1889868977398));
#181341=CARTESIAN_POINT('Ctrl Pts',(20.5349766171185,-20.0653556732191,
21.1833006273557));
#181342=CARTESIAN_POINT('Ctrl Pts',(20.5542939889263,-20.0334837838675,
21.1811348733856));
#181343=CARTESIAN_POINT('Ctrl Pts',(20.578279529162,-19.9914450901906,21.1782817260774));
#181344=CARTESIAN_POINT('Ctrl Pts',(20.5837231445138,-19.9817268369287,
21.1776224012635));
#181345=CARTESIAN_POINT('Ctrl Pts',(20.5924494090229,-19.965855719353,21.1765458481843));
#181346=CARTESIAN_POINT('Ctrl Pts',(20.5957788408715,-19.959728719179,21.1761302977831));
#181347=CARTESIAN_POINT('Ctrl Pts',(20.6021220740288,-19.9479168221561,
21.1753292269764));
#181348=CARTESIAN_POINT('Ctrl Pts',(20.6051403520067,-19.9422344075029,
21.174943871447));
#181349=CARTESIAN_POINT('Ctrl Pts',(20.6119900834686,-19.92919549933,21.1740596351986));
#181350=CARTESIAN_POINT('Ctrl Pts',(20.615804283385,-19.9218301054796,21.1735601516561));
#181351=CARTESIAN_POINT('Ctrl Pts',(20.6258185648125,-19.9022105666896,
21.1722295668705));
#181352=CARTESIAN_POINT('Ctrl Pts',(20.6319427775811,-19.8899183345578,
21.1713958232673));
#181353=CARTESIAN_POINT('Ctrl Pts',(20.6774820204886,-19.7962414414736,
21.1650403524921));
#181354=CARTESIAN_POINT('Ctrl Pts',(20.7117607596288,-19.7124765686798,
21.1593417739695));
#181355=CARTESIAN_POINT('Ctrl Pts',(20.7851821673454,-19.4941470710627,
21.144468198504));
#181356=CARTESIAN_POINT('Ctrl Pts',(20.8165236172352,-19.3574160158983,
21.135116863114));
#181357=CARTESIAN_POINT('Ctrl Pts',(20.8410813995823,-19.1639686555513,
21.1223459890741));
#181358=CARTESIAN_POINT('Ctrl Pts',(20.8458833598798,-19.1090740002333,
21.1187766099113));
#181359=CARTESIAN_POINT('Ctrl Pts',(20.8499084970286,-19.0256716074268,
21.1134918171265));
#181360=CARTESIAN_POINT('Ctrl Pts',(20.8507067513395,-18.997265727816,21.1117161926146));
#181361=CARTESIAN_POINT('Ctrl Pts',(20.8509881550703,-18.9619136032291,
21.1095435934988));
#181362=CARTESIAN_POINT('Ctrl Pts',(20.851009275974,-18.9549760302146,21.1091190226181));
#181363=CARTESIAN_POINT('Ctrl Pts',(20.8509887281256,-18.943995775956,21.108450002406));
#181364=CARTESIAN_POINT('Ctrl Pts',(20.8509695834442,-18.9399531739421,
21.1082043236695));
#181365=CARTESIAN_POINT('Ctrl Pts',(20.8509116405711,-18.9323294206652,
21.1077422381066));
#181366=CARTESIAN_POINT('Ctrl Pts',(20.8508753357138,-18.9287483567602,
21.107525700363));
#181367=CARTESIAN_POINT('Ctrl Pts',(20.8507715502681,-18.9205607228903,
21.1070317729593));
#181368=CARTESIAN_POINT('Ctrl Pts',(20.8506981199238,-18.9159542762498,
21.1067547192566));
#181369=CARTESIAN_POINT('Ctrl Pts',(20.8504631957205,-18.9037225650517,
21.1060211765708));
#181370=CARTESIAN_POINT('Ctrl Pts',(20.8502755294535,-18.8960977910171,
21.1055661137898));
#181371=CARTESIAN_POINT('Ctrl Pts',(20.8486704700771,-18.8426333170003,
21.102389630185));
#181372=CARTESIAN_POINT('Ctrl Pts',(20.8458049307357,-18.7968456285292,
21.0997433818247));
#181373=CARTESIAN_POINT('Ctrl Pts',(20.8378764030201,-18.7136402040259,
21.0950120349543));
#181374=CARTESIAN_POINT('Ctrl Pts',(20.8332961902683,-18.6761974474987,
21.0929116943981));
#181375=CARTESIAN_POINT('Ctrl Pts',(20.8083599867846,-18.5094499292422,
21.0836114693363));
#181376=CARTESIAN_POINT('Ctrl Pts',(20.7770394305811,-18.3820778286941,
21.0766340367471));
#181377=CARTESIAN_POINT('Ctrl Pts',(20.7052143912656,-18.1749503400491,
21.0645333126297));
#181378=CARTESIAN_POINT('Ctrl Pts',(20.6710804829987,-18.093391249084,21.0595612181679));
#181379=CARTESIAN_POINT('Ctrl Pts',(20.6228634134068,-17.9958068894792,
21.0532176350172));
#181380=CARTESIAN_POINT('Ctrl Pts',(20.6135045225415,-17.9775396544109,
21.0520126166617));
#181381=CARTESIAN_POINT('Ctrl Pts',(20.5997293308401,-17.9515893352124,
21.0502742671261));
#181382=CARTESIAN_POINT('Ctrl Pts',(20.5955279170785,-17.9437930547351,
21.0497485408595));
#181383=CARTESIAN_POINT('Ctrl Pts',(20.5881610424839,-17.930325881316,21.0488342716432));
#181384=CARTESIAN_POINT('Ctrl Pts',(20.5850181554353,-17.924642728623,21.0484465390221));
#181385=CARTESIAN_POINT('Ctrl Pts',(20.5789258966257,-17.9137450576527,
21.047699324946));
#181386=CARTESIAN_POINT('Ctrl Pts',(20.5759804390021,-17.9085284141219,
21.0473399870205));
#181387=CARTESIAN_POINT('Ctrl Pts',(20.5682085162118,-17.8948991601638,
21.0463967903315));
#181388=CARTESIAN_POINT('Ctrl Pts',(20.5633463524841,-17.8865071636666,
21.0458116441741));
#181389=CARTESIAN_POINT('Ctrl Pts',(20.5462830393813,-17.8575173275916,
21.0437748159947));
#181390=CARTESIAN_POINT('Ctrl Pts',(20.5337906375998,-17.8370938506119,
21.0423125608835));
#181391=CARTESIAN_POINT('Ctrl Pts',(20.437688250306,-17.6858043523982,21.0312702200361));
#181392=CARTESIAN_POINT('Ctrl Pts',(20.3402658860461,-17.5643046430061,
21.0211539584876));
#181393=CARTESIAN_POINT('Ctrl Pts',(20.1778803722248,-17.4020245537588,
21.0059870829959));
#181394=CARTESIAN_POINT('Ctrl Pts',(20.1225696484507,-17.3522846203843,
21.0010639598907));
#181395=CARTESIAN_POINT('Ctrl Pts',(20.028998481291,-17.276654713559,20.9932278202406));
#181396=CARTESIAN_POINT('Ctrl Pts',(19.9923064786629,-17.2489238869821,
20.9902670047035));
#181397=CARTESIAN_POINT('Ctrl Pts',(19.9410818214538,-17.2127697453463,
20.9863123316715));
#181398=CARTESIAN_POINT('Ctrl Pts',(19.9273112377688,-17.2032928406762,
20.9852661631811));
#181399=CARTESIAN_POINT('Ctrl Pts',(19.9035327472823,-17.1873402083815,
20.9834904469739));
#181400=CARTESIAN_POINT('Ctrl Pts',(19.8935799343699,-17.1807841978066,
20.9827562531052));
#181401=CARTESIAN_POINT('Ctrl Pts',(19.8793557607081,-17.1715858930414,
20.9817203767252));
#181402=CARTESIAN_POINT('Ctrl Pts',(19.875129755275,-17.1688743472027,20.9814142824737));
#181403=CARTESIAN_POINT('Ctrl Pts',(19.8678311048005,-17.1642278640575,
20.9808885509462));
#181404=CARTESIAN_POINT('Ctrl Pts',(19.8647630701667,-17.1622857590666,
20.9806684405972));
#181405=CARTESIAN_POINT('Ctrl Pts',(19.8588031819148,-17.1585345174327,
20.9802425906173));
#181406=CARTESIAN_POINT('Ctrl Pts',(19.8559119557867,-17.1567244782347,
20.9800367880116));
#181407=CARTESIAN_POINT('Ctrl Pts',(19.8481023035486,-17.1518615142039,
20.9794829568551));
#181408=CARTESIAN_POINT('Ctrl Pts',(19.8431756674405,-17.1488217361098,
20.9791357894279));
#181409=CARTESIAN_POINT('Ctrl Pts',(19.824860016079,-17.1376242850711,20.9778530720615));
#181410=CARTESIAN_POINT('Ctrl Pts',(19.811392596281,-17.1295949858659,20.9769255598791));
#181411=CARTESIAN_POINT('Ctrl Pts',(19.6817599742594,-17.0542471521348,
20.9681342241796));
#181412=CARTESIAN_POINT('Ctrl Pts',(19.5595112920428,-16.9979642118648,
20.9608716898857));
#181413=CARTESIAN_POINT('Ctrl Pts',(19.2810467922208,-16.9005973156725,
20.9448519428443));
#181414=CARTESIAN_POINT('Ctrl Pts',(19.1238293827648,-16.865007414114,20.9361045840124));
#181415=CARTESIAN_POINT('Ctrl Pts',(18.9455575971384,-16.8455146318888,
20.9256316173492));
#181416=CARTESIAN_POINT('Ctrl Pts',(18.9269818773604,-16.8437317094385,
20.9245344936359));
#181417=CARTESIAN_POINT('Ctrl Pts',(18.8998851475894,-16.8414920359134,
20.9229246681688));
#181418=CARTESIAN_POINT('Ctrl Pts',(18.8913807799546,-16.8408408313162,
20.9224180718565));
#181419=CARTESIAN_POINT('Ctrl Pts',(18.8764412597701,-16.8397876390288,
20.9215256834124));
#181420=CARTESIAN_POINT('Ctrl Pts',(18.8700077344895,-16.8393636221384,
20.9211405879492));
#181421=CARTESIAN_POINT('Ctrl Pts',(18.8574951701933,-16.8385963436045,
20.9203900242757));
#181422=CARTESIAN_POINT('Ctrl Pts',(18.8514163839996,-16.838249905147,20.9200246597673));
#181423=CARTESIAN_POINT('Ctrl Pts',(18.836854598859,-16.8374830175194,20.9191476427967));
#181424=CARTESIAN_POINT('Ctrl Pts',(18.8283704481463,-16.8370873888186,
20.9186352166053));
#181425=CARTESIAN_POINT('Ctrl Pts',(18.797586088843,-16.8358374739629,20.9167705181264));
#181426=CARTESIAN_POINT('Ctrl Pts',(18.7752757174883,-16.8352847894329,
20.9154088510575));
#181427=CARTESIAN_POINT('Ctrl Pts',(18.5696370358765,-16.8334428625074,
20.902759415006));
#181428=CARTESIAN_POINT('Ctrl Pts',(18.3869084940813,-16.855622073206,20.8906947770097));
#181429=CARTESIAN_POINT('Ctrl Pts',(18.1303751017278,-16.9212430484505,
20.873210704081));
#181430=CARTESIAN_POINT('Ctrl Pts',(18.0526121623917,-16.9459967132677,
20.8678505798224));
#181431=CARTESIAN_POINT('Ctrl Pts',(17.9424738267629,-16.9882025260496,
20.8603296450368));
#181432=CARTESIAN_POINT('Ctrl Pts',(17.9088201517948,-17.0021044161105,
20.8580420077422));
#181433=CARTESIAN_POINT('Ctrl Pts',(17.8686912632749,-17.0199063379301,
20.8553410607037));
#181434=CARTESIAN_POINT('Ctrl Pts',(17.8618590201806,-17.0229807559185,
20.8548821606062));
#181435=CARTESIAN_POINT('Ctrl Pts',(17.8512527308878,-17.0278213132715,
20.8541714267529));
#181436=CARTESIAN_POINT('Ctrl Pts',(17.8474674131566,-17.0295623982193,
20.8539181004372));
#181437=CARTESIAN_POINT('Ctrl Pts',(17.8404512827614,-17.0328146490806,
20.8534492048727));
#181438=CARTESIAN_POINT('Ctrl Pts',(17.8372191776505,-17.0343227909208,
20.8532334596927));
#181439=CARTESIAN_POINT('Ctrl Pts',(17.8299130309321,-17.0377544438658,
20.8527463458966));
#181440=CARTESIAN_POINT('Ctrl Pts',(17.8258413198539,-17.0396827906032,
20.8524752803585));
#181441=CARTESIAN_POINT('Ctrl Pts',(17.8135516627866,-17.045551229067,20.8516582496771));
#181442=CARTESIAN_POINT('Ctrl Pts',(17.8053528508338,-17.0495314623478,
20.8511147112901));
#181443=CARTESIAN_POINT('Ctrl Pts',(17.742406216224,-17.0805937132484,20.8469515463504));
#181444=CARTESIAN_POINT('Ctrl Pts',(17.6888224654806,-17.1099834118851,
20.8434650927345));
#181445=CARTESIAN_POINT('Ctrl Pts',(17.4971413360328,-17.2261791556759,
20.8309358352664));
#181446=CARTESIAN_POINT('Ctrl Pts',(17.3679310295523,-17.3265344579058,
20.822334812292));
#181447=CARTESIAN_POINT('Ctrl Pts',(17.1948920697157,-17.4962777335003,
20.8088862716257));
#181448=CARTESIAN_POINT('Ctrl Pts',(17.1414401068225,-17.5549561348151,
20.8043989609515));
#181449=CARTESIAN_POINT('Ctrl Pts',(17.0791842933686,-17.6315267840372,
20.7986403172648));
#181450=CARTESIAN_POINT('Ctrl Pts',(17.0671665414322,-17.6467296366283,
20.7975015884369));
#181451=CARTESIAN_POINT('Ctrl Pts',(17.0500837422399,-17.668960636741,20.7958420316206));
#181452=CARTESIAN_POINT('Ctrl Pts',(17.044850238435,-17.6758585304013,20.7953278661296));
#181453=CARTESIAN_POINT('Ctrl Pts',(17.0357827044756,-17.6879632815061,
20.7944268228756));
#181454=CARTESIAN_POINT('Ctrl Pts',(17.0319299155863,-17.6931559926538,
20.7940406860234));
#181455=CARTESIAN_POINT('Ctrl Pts',(17.024519245587,-17.7032401613848,20.7932915348351));
#181456=CARTESIAN_POINT('Ctrl Pts',(17.0209584160246,-17.708129381874,20.7929286403344));
#181457=CARTESIAN_POINT('Ctrl Pts',(17.0125342438771,-17.719801029225,20.792063066597));
#181458=CARTESIAN_POINT('Ctrl Pts',(17.007689987609,-17.7265970495051,20.7915596575451));
#181459=CARTESIAN_POINT('Ctrl Pts',(16.9905654135399,-17.7509242367281,
20.7897596025362));
#181460=CARTESIAN_POINT('Ctrl Pts',(16.9785112585108,-17.768612332288,20.7884543812602));
#181461=CARTESIAN_POINT('Ctrl Pts',(16.8760651530056,-17.923950817612,20.7770190472491));
#181462=CARTESIAN_POINT('Ctrl Pts',(16.8018176257906,-18.0714332124806,
20.7662793014811));
#181463=CARTESIAN_POINT('Ctrl Pts',(16.7454193641621,-18.2258897778089,
20.7554136941352));
#181464=CARTESIAN_POINT('',(16.6170002905217,-18.953109084689,21.2890562789773));
#181465=CARTESIAN_POINT('Ctrl Pts',(16.6170002905217,-18.953109084689,21.2890562789773));
#181466=CARTESIAN_POINT('Ctrl Pts',(16.6170426459378,-19.0339562954196,
21.2842160179952));
#181467=CARTESIAN_POINT('Ctrl Pts',(16.6217204202766,-19.1146414522941,
21.2793757570132));
#181468=CARTESIAN_POINT('Ctrl Pts',(16.6309534061133,-19.1946603056566,
21.2745354960311));
#181469=CARTESIAN_POINT('Ctrl Pts',(16.6402204413664,-19.2749742526441,
21.2696773851287));
#181470=CARTESIAN_POINT('Ctrl Pts',(16.6540762119897,-19.354616695186,21.2648192742263));
#181471=CARTESIAN_POINT('Ctrl Pts',(16.6723897124588,-19.4330946084755,
21.2599611633239));
#181472=CARTESIAN_POINT('Ctrl Pts',(16.6907932575821,-19.5119583855476,
21.2550791658403));
#181473=CARTESIAN_POINT('Ctrl Pts',(16.7136983366374,-19.5896458842218,
21.2501971683567));
#181474=CARTESIAN_POINT('Ctrl Pts',(16.7409237561882,-19.6656778589483,
21.2453151708731));
#181475=CARTESIAN_POINT('Ctrl Pts',(16.7538532441133,-19.7017858240547,
21.2429966858486));
#181476=CARTESIAN_POINT('Ctrl Pts',(16.7677564318017,-19.7375207423804,
21.240678200824));
#181477=CARTESIAN_POINT('Ctrl Pts',(16.7826102745739,-19.7728331983426,
21.2383597157995));
#181478=CARTESIAN_POINT('Ctrl Pts',(16.810725579552,-19.8396724993995,21.2339712949342));
#181479=CARTESIAN_POINT('Ctrl Pts',(16.842333782473,-19.9051959888482,21.2295828740689));
#181480=CARTESIAN_POINT('Ctrl Pts',(16.8772900904223,-19.9690139191162,
21.2251944532036));
#181481=CARTESIAN_POINT('Ctrl Pts',(16.9121945323206,-20.0327371602073,
21.2208125436112));
#181482=CARTESIAN_POINT('Ctrl Pts',(16.9504369878248,-20.0947594462028,
21.2164306340188));
#181483=CARTESIAN_POINT('Ctrl Pts',(16.9918247589115,-20.1547112826186,
21.2120487244264));
#181484=CARTESIAN_POINT('Ctrl Pts',(17.0331639104988,-20.2145926917514,
21.2076719623992));
#181485=CARTESIAN_POINT('Ctrl Pts',(17.0776407650442,-20.2724080879841,
21.203295200372));
#181486=CARTESIAN_POINT('Ctrl Pts',(17.1250177576845,-20.3278143566315,
21.1989184383448));
#181487=CARTESIAN_POINT('Ctrl Pts',(17.1723647132798,-20.3831854976676,
21.1945444511876));
#181488=CARTESIAN_POINT('Ctrl Pts',(17.2226078460713,-20.4361501759871,
21.1901704640305));
#181489=CARTESIAN_POINT('Ctrl Pts',(17.2754683635278,-20.4863971016037,
21.1857964768734));
#181490=CARTESIAN_POINT('Ctrl Pts',(17.3283128004351,-20.5366287417445,
21.1814238203145));
#181491=CARTESIAN_POINT('Ctrl Pts',(17.3837726918675,-20.5841439384587,
21.1770511637557));
#181492=CARTESIAN_POINT('Ctrl Pts',(17.4415325036287,-20.6286683544529,
21.1726785071969));
#181493=CARTESIAN_POINT('Ctrl Pts',(17.4992937927453,-20.6731939092732,
21.1683057387962));
#181494=CARTESIAN_POINT('Ctrl Pts',(17.5593547357629,-20.7147282386116,
21.1639329703954));
#181495=CARTESIAN_POINT('Ctrl Pts',(17.6213681906132,-20.7530384384407,
21.1595602019947));
#181496=CARTESIAN_POINT('Ctrl Pts',(17.6834459816507,-20.7913883833894,
21.1551828970422));
#181497=CARTESIAN_POINT('Ctrl Pts',(17.7474799176421,-20.8265072664897,
21.1508055920898));
#181498=CARTESIAN_POINT('Ctrl Pts',(17.8130961649932,-20.858206999953,21.1464282871373));
#181499=CARTESIAN_POINT('Ctrl Pts',(17.8787482388868,-20.8899240415053,
21.1420485921716));
#181500=CARTESIAN_POINT('Ctrl Pts',(17.945983899379,-20.9182180292927,21.1376688972058));
#181501=CARTESIAN_POINT('Ctrl Pts',(18.0144096452291,-20.9429492010899,
21.1332892022401));
#181502=CARTESIAN_POINT('Ctrl Pts',(18.0829566199304,-20.9677241887274,
21.1289017478355));
#181503=CARTESIAN_POINT('Ctrl Pts',(18.1526974286133,-20.9889236147803,
21.124514293431));
#181504=CARTESIAN_POINT('Ctrl Pts',(18.2232243125218,-21.0064578839882,
21.1201268390264));
#181505=CARTESIAN_POINT('Ctrl Pts',(18.2711425297296,-21.018371226446,21.1171458623903));
#181506=CARTESIAN_POINT('Ctrl Pts',(18.3194233717923,-21.0285936957892,
21.1141648857542));
#181507=CARTESIAN_POINT('Ctrl Pts',(18.3679374554048,-21.0371108396065,
21.1111839091181));
#181508=CARTESIAN_POINT('Ctrl Pts',(18.4393551978057,-21.0496489550946,
21.1067956035861));
#181509=CARTESIAN_POINT('Ctrl Pts',(18.5115571842922,-21.0585380615907,
21.102407298054));
#181510=CARTESIAN_POINT('Ctrl Pts',(18.5841373443173,-21.0636889412107,
21.098018992522));
#181511=CARTESIAN_POINT('Ctrl Pts',(18.6566098258321,-21.0688321790862,
21.0936371973945));
#181512=CARTESIAN_POINT('Ctrl Pts',(18.7294588899518,-21.07024816573,21.089255402267));
#181513=CARTESIAN_POINT('Ctrl Pts',(18.8022695648095,-21.067898926348,21.0848736071394));
#181514=CARTESIAN_POINT('Ctrl Pts',(18.8749947356317,-21.0655524457572,
21.080496957702));
#181515=CARTESIAN_POINT('Ctrl Pts',(18.9476811270357,-21.0594495382254,
21.0761203082645));
#181516=CARTESIAN_POINT('Ctrl Pts',(19.0199116621127,-21.0496042337553,
21.0717436588271));
#181517=CARTESIAN_POINT('Ctrl Pts',(19.0920964218622,-21.0397651686413,
21.0673697830443));
#181518=CARTESIAN_POINT('Ctrl Pts',(19.1638254217295,-21.0261884773497,
21.0629959072615));
#181519=CARTESIAN_POINT('Ctrl Pts',(19.2346860285047,-21.0089400819811,
21.0586220314788));
#181520=CARTESIAN_POINT('Ctrl Pts',(19.3055251008402,-20.9916969283757,
21.0542494849107));
#181521=CARTESIAN_POINT('Ctrl Pts',(19.3754958356271,-20.9707843999674,
21.0498769383427));
#181522=CARTESIAN_POINT('Ctrl Pts',(19.4441967837545,-20.9463193145394,
21.0455043917747));
#181523=CARTESIAN_POINT('Ctrl Pts',(19.512899513531,-20.9218535946485,21.0411317318117));
#181524=CARTESIAN_POINT('Ctrl Pts',(19.5803319375393,-20.8938352985226,
21.0367590718487));
#181525=CARTESIAN_POINT('Ctrl Pts',(19.6461103373975,-20.8624302479841,
21.0323864118857));
#181526=CARTESIAN_POINT('Ctrl Pts',(19.7119570287599,-20.8309925925458,
21.0280092122026));
#181527=CARTESIAN_POINT('Ctrl Pts',(19.7761458312172,-20.7961613707408,
21.0236320125194));
#181528=CARTESIAN_POINT('Ctrl Pts',(19.8383162627571,-20.7581491056417,
21.0192548128363));
#181529=CARTESIAN_POINT('Ctrl Pts',(19.9005206631089,-20.7201160713208,
21.0148752215295));
#181530=CARTESIAN_POINT('Ctrl Pts',(19.9607040986315,-20.6788988059761,
21.0104956302228));
#181531=CARTESIAN_POINT('Ctrl Pts',(20.0185360770276,-20.6347525269078,
21.006116038916));
#181532=CARTESIAN_POINT('Ctrl Pts',(20.0764705677122,-20.5905279946616,
21.0017286843969));
#181533=CARTESIAN_POINT('Ctrl Pts',(20.1320449095234,-20.5433643929912,
20.9973413298778));
#181534=CARTESIAN_POINT('Ctrl Pts',(20.1849630763877,-20.4935560810297,
20.9929539753587));
#181535=CARTESIAN_POINT('Ctrl Pts',(20.2209300198673,-20.4597028157469,
20.989972017718));
#181536=CARTESIAN_POINT('Ctrl Pts',(20.2556706968499,-20.4246286057098,
20.9869900600773));
#181537=CARTESIAN_POINT('Ctrl Pts',(20.2891028444412,-20.3884345245123,
20.9840081024366));
#181538=CARTESIAN_POINT('Ctrl Pts',(20.338299896607,-20.3351731509824,20.9796200048666));
#181539=CARTESIAN_POINT('Ctrl Pts',(20.3848536071561,-20.2792773791151,
20.9752319072966));
#181540=CARTESIAN_POINT('Ctrl Pts',(20.428469154839,-20.2210403001084,20.9708438097266));
#181541=CARTESIAN_POINT('Ctrl Pts',(20.472019950475,-20.1628896804098,20.9664622267669));
#181542=CARTESIAN_POINT('Ctrl Pts',(20.5126409556541,-20.1024050366756,
20.9620806438073));
#181543=CARTESIAN_POINT('Ctrl Pts',(20.5500756139241,-20.0399146862278,
20.9576990608477));
#181544=CARTESIAN_POINT('Ctrl Pts',(20.5874662643004,-19.9774977989509,
20.953322628843));
#181545=CARTESIAN_POINT('Ctrl Pts',(20.621677762229,-19.9130803007029,20.9489461968383));
#181546=CARTESIAN_POINT('Ctrl Pts',(20.6524961365199,-19.8470204322574,
20.9445697648336));
#181547=CARTESIAN_POINT('Ctrl Pts',(20.6832949569897,-19.7810024778609,
20.9401961096128));
#181548=CARTESIAN_POINT('Ctrl Pts',(20.7107047219756,-19.7133446569422,
20.9358224543921));
#181549=CARTESIAN_POINT('Ctrl Pts',(20.7345574961774,-19.6444295664459,
20.9314487991714));
#181550=CARTESIAN_POINT('Ctrl Pts',(20.7584030058596,-19.5755354644946,
20.9270764759762));
#181551=CARTESIAN_POINT('Ctrl Pts',(20.7786935177564,-19.5053853087556,
20.922704152781));
#181552=CARTESIAN_POINT('Ctrl Pts',(20.7953099439741,-19.4343798450118,
20.9183318295858));
#181553=CARTESIAN_POINT('Ctrl Pts',(20.8119267916513,-19.3633725802829,
20.9139593954909));
#181554=CARTESIAN_POINT('Ctrl Pts',(20.8248692606565,-19.2915104346493,
20.9095869613959));
#181555=CARTESIAN_POINT('Ctrl Pts',(20.8340690642333,-19.2192057736098,
20.905214527301));
#181556=CARTESIAN_POINT('Ctrl Pts',(20.8432784147593,-19.1468260795634,
20.9008375557824));
#181557=CARTESIAN_POINT('Ctrl Pts',(20.8487372843852,-19.0740034328328,
20.8964605842638));
#181558=CARTESIAN_POINT('Ctrl Pts',(20.8504292318327,-19.0011559421033,
20.8920836127452));
#181559=CARTESIAN_POINT('Ctrl Pts',(20.8521221031445,-18.9282686740168,
20.8877042512424));
#181560=CARTESIAN_POINT('Ctrl Pts',(20.8500439708189,-18.8553570174668,
20.8833248897395));
#181561=CARTESIAN_POINT('Ctrl Pts',(20.8442305256586,-18.7828369763254,
20.8789455282366));
#181562=CARTESIAN_POINT('Ctrl Pts',(20.8384067752504,-18.7101883819803,
20.8745584036252));
#181563=CARTESIAN_POINT('Ctrl Pts',(20.8288345526933,-18.6379332679819,
20.8701712790138));
#181564=CARTESIAN_POINT('Ctrl Pts',(20.8156011171495,-18.5664798460756,
20.8657841544023));
#181565=CARTESIAN_POINT('Ctrl Pts',(20.8066002449081,-18.5178799855435,
20.86280020152));
#181566=CARTESIAN_POINT('Ctrl Pts',(20.7959066970833,-18.4696507896963,
20.8598162486376));
#181567=CARTESIAN_POINT('Ctrl Pts',(20.7835610193721,-18.4219163953954,
20.8568322957552));
#181568=CARTESIAN_POINT('Ctrl Pts',(20.7654052821341,-18.3517174852658,
20.8524440502713));
#181569=CARTESIAN_POINT('Ctrl Pts',(20.7436033945615,-18.2823154158224,
20.8480558047873));
#181570=CARTESIAN_POINT('Ctrl Pts',(20.7182422504866,-18.2141167494895,
20.8436675593033));
#181571=CARTESIAN_POINT('Ctrl Pts',(20.6929187442307,-18.1460192950363,
20.8392858263012));
#181572=CARTESIAN_POINT('Ctrl Pts',(20.6640466341085,-18.0791221467405,
20.834904093299));
#181573=CARTESIAN_POINT('Ctrl Pts',(20.6317631446628,-18.0138187559115,
20.8305223602969));
#181574=CARTESIAN_POINT('Ctrl Pts',(20.599517588069,-17.9485920960646,20.8261457757973));
#181575=CARTESIAN_POINT('Ctrl Pts',(20.563868827466,-17.8849559039143,20.8217691912977));
#181576=CARTESIAN_POINT('Ctrl Pts',(20.525002297749,-17.823284017364,20.8173926067981));
#181577=CARTESIAN_POINT('Ctrl Pts',(20.4861604147302,-17.7616512392287,
20.813018797652));
#181578=CARTESIAN_POINT('Ctrl Pts',(20.4441050677791,-17.7019807022678,
20.8086449885059));
#181579=CARTESIAN_POINT('Ctrl Pts',(20.3990670884687,-17.6446207165102,
20.8042711793597));
#181580=CARTESIAN_POINT('Ctrl Pts',(20.3540428128668,-17.5872781836785,
20.7998987010328));
#181581=CARTESIAN_POINT('Ctrl Pts',(20.3060380043386,-17.5322451854803,
20.7955262227058));
#181582=CARTESIAN_POINT('Ctrl Pts',(20.2553251935424,-17.47983878074,20.7911537443788));
#181583=CARTESIAN_POINT('Ctrl Pts',(20.2046110851032,-17.4274310350208,
20.7867811541686));
#181584=CARTESIAN_POINT('Ctrl Pts',(20.1511891736979,-17.3776503614482,
20.7824085639583));
#181585=CARTESIAN_POINT('Ctrl Pts',(20.0953692567414,-17.3307773913496,
20.778035973748));
#181586=CARTESIAN_POINT('Ctrl Pts',(20.0394914100484,-17.2838557766281,
20.7736588456772));
#181587=CARTESIAN_POINT('Ctrl Pts',(19.9812109592545,-17.2398482010919,
20.7692817176064));
#181588=CARTESIAN_POINT('Ctrl Pts',(19.9208705927643,-17.1989948100387,
20.7649045895356));
#181589=CARTESIAN_POINT('Ctrl Pts',(19.8604972727169,-17.1581191078091,
20.7605250709931));
#181590=CARTESIAN_POINT('Ctrl Pts',(19.7980622103152,-17.120401269318,20.7561455524505));
#181591=CARTESIAN_POINT('Ctrl Pts',(19.7339345415247,-17.086036465344,20.751766033908));
#181592=CARTESIAN_POINT('Ctrl Pts',(19.6696932144357,-17.0516107540391,
20.7473787532148));
#181593=CARTESIAN_POINT('Ctrl Pts',(19.6037537269743,-17.0205501505905,
20.7429914725216));
#181594=CARTESIAN_POINT('Ctrl Pts',(19.5365065755261,-16.9930022470055,
20.7386041918285));
#181595=CARTESIAN_POINT('Ctrl Pts',(19.4907905185625,-16.9742745908536,
20.7356216242436));
#181596=CARTESIAN_POINT('Ctrl Pts',(19.4444705161313,-16.9571693364,20.7326390566587));
#181597=CARTESIAN_POINT('Ctrl Pts',(19.3976727117744,-16.9417195390578,
20.7296564890738));
#181598=CARTESIAN_POINT('Ctrl Pts',(19.3288196246044,-16.9189884246865,
20.7252682706791));
#181599=CARTESIAN_POINT('Ctrl Pts',(19.2586629666827,-16.8997544121691,
20.7208800522844));
#181600=CARTESIAN_POINT('Ctrl Pts',(19.1875916213734,-16.884164503395,20.7164918338897));
#181601=CARTESIAN_POINT('Ctrl Pts',(19.1166257528894,-16.8685977315697,
20.7121101280401));
#181602=CARTESIAN_POINT('Ctrl Pts',(19.0447483590908,-16.8566644299584,
20.7077284221905));
#181603=CARTESIAN_POINT('Ctrl Pts',(18.9723645424295,-16.8484621836267,
20.7033467163409));
#181604=CARTESIAN_POINT('Ctrl Pts',(18.9000657760626,-16.8402695748564,
20.6989701589539));
#181605=CARTESIAN_POINT('Ctrl Pts',(18.827262245817,-16.8357993666553,20.6945936015669));
#181606=CARTESIAN_POINT('Ctrl Pts',(18.7543686580674,-16.8350979905134,
20.69021704418));
#181607=CARTESIAN_POINT('Ctrl Pts',(18.6815212944638,-16.8343970591364,
20.6858432621074));
#181608=CARTESIAN_POINT('Ctrl Pts',(18.6085844678331,-16.8374602225037,
20.6814694800349));
#181609=CARTESIAN_POINT('Ctrl Pts',(18.5359759922545,-16.8442819229422,
20.6770956979624));
#181610=CARTESIAN_POINT('Ctrl Pts',(18.4633896080828,-16.8511015478521,
20.6727232466298));
#181611=CARTESIAN_POINT('Ctrl Pts',(18.3911318565986,-16.8616773944406,
20.6683507952972));
#181612=CARTESIAN_POINT('Ctrl Pts',(18.3196168456417,-16.8759519270055,
20.6639783439647));
#181613=CARTESIAN_POINT('Ctrl Pts',(18.2481000027887,-16.8902268252204,
20.6596057806294));
#181614=CARTESIAN_POINT('Ctrl Pts',(18.1773264108895,-16.9082005011352,
20.6552332172941));
#181615=CARTESIAN_POINT('Ctrl Pts',(18.1076997198728,-16.9297643660759,
20.6508606539588));
#181616=CARTESIAN_POINT('Ctrl Pts',(18.0380007641074,-16.951350611906,20.6464835523899));
#181617=CARTESIAN_POINT('Ctrl Pts',(17.9694515476174,-16.9765343433904,
20.642106450821));
#181618=CARTESIAN_POINT('Ctrl Pts',(17.9024394812806,-17.0051574014042,
20.6377293492521));
#181619=CARTESIAN_POINT('Ctrl Pts',(17.8353908149959,-17.0337960924599,
20.6333498570437));
#181620=CARTESIAN_POINT('Ctrl Pts',(17.7698814039051,-17.0658776377278,
20.6289703648353));
#181621=CARTESIAN_POINT('Ctrl Pts',(17.7062751578752,-17.1011972960687,
20.624590872627));
#181622=CARTESIAN_POINT('Ctrl Pts',(17.6425561688023,-17.1365795590437,
20.6202036177018));
#181623=CARTESIAN_POINT('Ctrl Pts',(17.5807474907214,-17.1752111409601,
20.6158163627765));
#181624=CARTESIAN_POINT('Ctrl Pts',(17.5211845891613,-17.2168435865225,
20.6114291078513));
#181625=CARTESIAN_POINT('Ctrl Pts',(17.480688941821,-17.2451486688682,20.608446299365));
#181626=CARTESIAN_POINT('Ctrl Pts',(17.4412307372722,-17.2748399742566,
20.6054634908787));
#181627=CARTESIAN_POINT('Ctrl Pts',(17.4029060721978,-17.305829305519,20.6024806823923));
#181628=CARTESIAN_POINT('Ctrl Pts',(17.3472665725173,-17.3508194152439,
20.5981502604174));
#181629=CARTESIAN_POINT('Ctrl Pts',(17.2937883055875,-17.3987327323833,
20.5938198384424));
#181630=CARTESIAN_POINT('Ctrl Pts',(17.2428007358767,-17.4493311227425,
20.5894894164674));
#181631=CARTESIAN_POINT('Ctrl Pts',(17.1918849324912,-17.4998582945566,
20.5851650896735));
#181632=CARTESIAN_POINT('Ctrl Pts',(17.1434532240763,-17.553062699864,20.5808407628797));
#181633=CARTESIAN_POINT('Ctrl Pts',(17.0978028464621,-17.608665389877,20.5765164360858));
#181634=CARTESIAN_POINT('Ctrl Pts',(17.0522038396047,-17.6642055097116,
20.5721969754935));
#181635=CARTESIAN_POINT('Ctrl Pts',(17.0093802643348,-17.7221381759371,
20.5678775149012));
#181636=CARTESIAN_POINT('Ctrl Pts',(16.9695918504464,-17.7821483505209,
20.563558054309));
#181637=CARTESIAN_POINT('Ctrl Pts',(16.9298290257308,-17.8421199306856,
20.5592413716968));
#181638=CARTESIAN_POINT('Ctrl Pts',(16.8930977626958,-17.9041659555432,
20.5549246890847));
#181639=CARTESIAN_POINT('Ctrl Pts',(16.8596158552961,-17.9679405109026,
20.5506080064725));
#181640=CARTESIAN_POINT('Ctrl Pts',(16.8261394677777,-18.031704552286,20.5462920355157));
#181641=CARTESIAN_POINT('Ctrl Pts',(16.7959116072599,-18.0971961216295,
20.5419760645588));
#181642=CARTESIAN_POINT('Ctrl Pts',(16.7691044222789,-18.164044183566,20.5376600936019));
#181643=CARTESIAN_POINT('Ctrl Pts',(16.7608869615361,-18.184535754206,20.5363370780771));
#181644=CARTESIAN_POINT('Ctrl Pts',(16.7529905929685,-18.2051546356672,
20.5350140625523));
#181645=CARTESIAN_POINT('Ctrl Pts',(16.7454193692319,-18.2258897639242,
20.5336910470276));
#181646=CARTESIAN_POINT('Ctrl Pts',(16.7454193692319,-18.2258897639242,
21.3335535355786));
#181647=CARTESIAN_POINT('Ctrl Pts',(16.7201109656642,-18.2952012797656,
21.3291191852467));
#181648=CARTESIAN_POINT('Ctrl Pts',(16.6984027965461,-18.3659130286271,
21.3246848349147));
#181649=CARTESIAN_POINT('Ctrl Pts',(16.6804408864183,-18.4376227386191,
21.3202504845828));
#181650=CARTESIAN_POINT('Ctrl Pts',(16.6624933610866,-18.509275019889,21.3158196855004));
#181651=CARTESIAN_POINT('Ctrl Pts',(16.6482862472522,-18.581923225276,21.311388886418));
#181652=CARTESIAN_POINT('Ctrl Pts',(16.637915803284,-18.6551498016211,21.3069580873356));
#181653=CARTESIAN_POINT('Ctrl Pts',(16.6275504569996,-18.7283403827929,
21.3025294662518));
#181654=CARTESIAN_POINT('Ctrl Pts',(16.6210180978407,-18.8021083105054,
21.298100845168));
#181655=CARTESIAN_POINT('Ctrl Pts',(16.618363660142,-18.8760271267351,21.2936722240842));
#181656=CARTESIAN_POINT('Ctrl Pts',(16.6174414213416,-18.9017089502108,
21.2921335757303));
#181657=CARTESIAN_POINT('Ctrl Pts',(16.6169868263616,-18.9274089350833,
21.2905949273764));
#181658=CARTESIAN_POINT('Ctrl Pts',(16.6170002905213,-18.9531090839331,
21.2890562790225));
#181659=CARTESIAN_POINT('Origin',(18.734,19.211,0.));
#181660=CARTESIAN_POINT('',(16.7454193623258,19.9371102171621,0.755484062589681));
#181661=CARTESIAN_POINT('',(16.7454193623539,19.9371102172391,0.534177402122747));
#181662=CARTESIAN_POINT('',(16.7454193623258,19.9371102171621,0.));
#181663=CARTESIAN_POINT('',(16.6170002905282,19.2121090969791,0.710943721022754));
#181664=CARTESIAN_POINT('Ctrl Pts',(16.6170002905282,19.2121090969791,0.710943721022754));
#181665=CARTESIAN_POINT('Ctrl Pts',(16.6170426220575,19.2929098178344,0.715781198916212));
#181666=CARTESIAN_POINT('Ctrl Pts',(16.6217150381803,19.3735486726215,0.72061867680967));
#181667=CARTESIAN_POINT('Ctrl Pts',(16.6309374842428,19.4535222769504,0.725456154703128));
#181668=CARTESIAN_POINT('Ctrl Pts',(16.6404786393294,19.5362596067819,0.730460806017553));
#181669=CARTESIAN_POINT('Ctrl Pts',(16.6548898616796,19.6182845120318,0.735465457331979));
#181670=CARTESIAN_POINT('Ctrl Pts',(16.6740271613156,19.6990582996761,0.740470108646404));
#181671=CARTESIAN_POINT('Ctrl Pts',(16.6931644609517,19.7798320873204,0.74547475996083));
#181672=CARTESIAN_POINT('Ctrl Pts',(16.717027633524,19.8593544704023,0.750479411275255));
#181673=CARTESIAN_POINT('Ctrl Pts',(16.7454193623258,19.9371102171621,0.755484062589681));
#181674=CARTESIAN_POINT('',(17.1140596925741,20.5738948603531,2.19263333745477E-7));
#181675=CARTESIAN_POINT('Ctrl Pts',(17.1140596925741,20.5738948603531,2.19263333745477E-7));
#181676=CARTESIAN_POINT('Ctrl Pts',(17.1607064305025,20.6293392920392,0.00438522669745755));
#181677=CARTESIAN_POINT('Ctrl Pts',(17.2102945911146,20.6824950671961,0.00877023413158137));
#181678=CARTESIAN_POINT('Ctrl Pts',(17.2625707969829,20.7330332126824,0.0131552415657052));
#181679=CARTESIAN_POINT('Ctrl Pts',(17.3147693813982,20.7834963174457,0.017533737994626));
#181680=CARTESIAN_POINT('Ctrl Pts',(17.3696477435684,20.8313491749509,0.0219122344235468));
#181681=CARTESIAN_POINT('Ctrl Pts',(17.4269127458044,20.876296342973,0.0262907308524677));
#181682=CARTESIAN_POINT('Ctrl Pts',(17.4841103523032,20.9211906122366,0.0306640741864277));
#181683=CARTESIAN_POINT('Ctrl Pts',(17.5436886409258,20.9631856884277,0.0350374175203878));
#181684=CARTESIAN_POINT('Ctrl Pts',(17.605319441071,21.0020246218005,0.0394107608543478));
#181685=CARTESIAN_POINT('Ctrl Pts',(17.6669112432928,21.0408389791862,0.0437813368819024));
#181686=CARTESIAN_POINT('Ctrl Pts',(17.7305525723991,21.0765008992432,0.0481519129094571));
#181687=CARTESIAN_POINT('Ctrl Pts',(17.7958853222654,21.10879605106,0.0525224889370117));
#181688=CARTESIAN_POINT('Ctrl Pts',(17.8611983685245,21.1410814630298,0.0568917468490216));
#181689=CARTESIAN_POINT('Ctrl Pts',(17.9282013899053,21.1700019086929,0.0612610047610315));
#181690=CARTESIAN_POINT('Ctrl Pts',(17.9965121600447,21.1953892475817,0.0656302626730415));
#181691=CARTESIAN_POINT('Ctrl Pts',(18.0648249509204,21.2207773374667,0.069999649834336));
#181692=CARTESIAN_POINT('Ctrl Pts',(18.134445113711,21.242631946831,0.0743690369956306));
#181693=CARTESIAN_POINT('Ctrl Pts',(18.2049725448517,21.260833883928,0.0787384241569251));
#181694=CARTESIAN_POINT('Ctrl Pts',(18.275571771191,21.2790543501514,0.0831122592474014));
#181695=CARTESIAN_POINT('Ctrl Pts',(18.3470796408086,21.2936146004556,0.0874860943378777));
#181696=CARTESIAN_POINT('Ctrl Pts',(18.4190839151667,21.3044461682865,0.091859929428354));
#181697=CARTESIAN_POINT('Ctrl Pts',(18.4911280120912,21.3152837266066,0.0962361835049216));
#181698=CARTESIAN_POINT('Ctrl Pts',(18.5636685792402,21.322388450086,0.100612437581489));
#181699=CARTESIAN_POINT('Ctrl Pts',(18.6362889712808,21.3257438508875,0.104988691658057));
#181700=CARTESIAN_POINT('Ctrl Pts',(18.7090335036841,21.3291049875528,0.109372426688014));
#181701=CARTESIAN_POINT('Ctrl Pts',(18.7818576501797,21.3287040083353,0.113756161717971));
#181702=CARTESIAN_POINT('Ctrl Pts',(18.854346170805,21.3245765420662,0.118139896747928));
#181703=CARTESIAN_POINT('Ctrl Pts',(18.8963545400865,21.3221846029601,0.120680348096384));
#181704=CARTESIAN_POINT('Ctrl Pts',(18.9382502971219,21.318542128427,0.123220799444841));
#181705=CARTESIAN_POINT('Ctrl Pts',(18.9799541345816,21.3136639207639,0.125761250793297));
#181706=CARTESIAN_POINT('Ctrl Pts',(19.0521147654861,21.3052231017867,0.130157023059194));
#181707=CARTESIAN_POINT('Ctrl Pts',(19.1239757191856,21.2930474831033,0.134552795325092));
#181708=CARTESIAN_POINT('Ctrl Pts',(19.1951211491521,21.2771694717047,0.138948567590989));
#181709=CARTESIAN_POINT('Ctrl Pts',(19.2661637519632,21.2613144089446,0.143337986606115));
#181710=CARTESIAN_POINT('Ctrl Pts',(19.336492418998,21.2417676813877,0.14772740562124));
#181711=CARTESIAN_POINT('Ctrl Pts',(19.4056976665711,21.2186133205184,0.152116824636366));
#181712=CARTESIAN_POINT('Ctrl Pts',(19.4748248958988,21.1954850626206,0.156501295258381));
#181713=CARTESIAN_POINT('Ctrl Pts',(19.5428307683091,21.1687574028734,0.160885765880397));
#181714=CARTESIAN_POINT('Ctrl Pts',(19.60931884804,21.1385647626645,0.165270236502412));
#181715=CARTESIAN_POINT('Ctrl Pts',(19.6757666435217,21.1083904157775,0.169652050631602));
#181716=CARTESIAN_POINT('Ctrl Pts',(19.7406980347466,21.0747554526422,0.174033864760792));
#181717=CARTESIAN_POINT('Ctrl Pts',(19.8037358627713,21.0378426817602,0.178415678889982));
#181718=CARTESIAN_POINT('Ctrl Pts',(19.8667560838771,21.0009402208807,0.182796269146952));
#181719=CARTESIAN_POINT('Ctrl Pts',(19.9278833775877,20.9607620127547,0.187176859403921));
#181720=CARTESIAN_POINT('Ctrl Pts',(19.9867660017252,20.9175363590974,0.19155744966089));
#181721=CARTESIAN_POINT('Ctrl Pts',(20.0456514086938,20.8743086625676,0.195938246947401));
#181722=CARTESIAN_POINT('Ctrl Pts',(20.10229154935,20.828033520426,0.200319044233912));
#181723=CARTESIAN_POINT('Ctrl Pts',(20.1563657971913,20.7789810391011,0.204699841520423));
#181724=CARTESIAN_POINT('Ctrl Pts',(20.2104971638002,20.7298767435135,0.209085266254418));
#181725=CARTESIAN_POINT('Ctrl Pts',(20.2620568697779,20.6779895750515,0.213470690988413));
#181726=CARTESIAN_POINT('Ctrl Pts',(20.3107599897288,20.6236276702622,0.217856115722409));
#181727=CARTESIAN_POINT('Ctrl Pts',(20.3594903544992,20.569235355095,0.222243993689488));
#181728=CARTESIAN_POINT('Ctrl Pts',(20.405360649667,20.5123659213335,0.226631871656568));
#181729=CARTESIAN_POINT('Ctrl Pts',(20.4481269507233,20.4533597694727,0.231019749623648));
#181730=CARTESIAN_POINT('Ctrl Pts',(20.490968988079,20.3942491216074,0.2354153982333));
#181731=CARTESIAN_POINT('Ctrl Pts',(20.5306957923998,20.3329946025316,0.239811046842951));
#181732=CARTESIAN_POINT('Ctrl Pts',(20.5671076961723,20.2699641987498,0.244206695452603));
#181733=CARTESIAN_POINT('Ctrl Pts',(20.5912140439174,20.2282351850302,0.247116816126646));
#181734=CARTESIAN_POINT('Ctrl Pts',(20.613868403521,20.1857283140019,0.250026936800689));
#181735=CARTESIAN_POINT('Ctrl Pts',(20.6350244604073,20.1425551518472,0.252937057474731));
#181736=CARTESIAN_POINT('Ctrl Pts',(20.6668851126084,20.0775371236191,0.257319648387442));
#181737=CARTESIAN_POINT('Ctrl Pts',(20.6954700480251,20.010752620059,0.261702239300152));
#181738=CARTESIAN_POINT('Ctrl Pts',(20.720580205096,19.9425655054202,0.266084830212863));
#181739=CARTESIAN_POINT('Ctrl Pts',(20.745652583015,19.8744809807952,0.270460827356878));
#181740=CARTESIAN_POINT('Ctrl Pts',(20.7672603940222,19.8049984839899,0.274836824500893));
#181741=CARTESIAN_POINT('Ctrl Pts',(20.7852512551748,19.7345048119586,0.279212821644908));
#181742=CARTESIAN_POINT('Ctrl Pts',(20.8032205628375,19.6640955930636,0.283583576237746));
#181743=CARTESIAN_POINT('Ctrl Pts',(20.8175814089924,19.5926780716229,0.287954330830584));
#181744=CARTESIAN_POINT('Ctrl Pts',(20.8282307375361,19.5206556441581,0.292325085423422));
#181745=CARTESIAN_POINT('Ctrl Pts',(20.8388731698584,19.4486798564987,0.296693009632014));
#181746=CARTESIAN_POINT('Ctrl Pts',(20.845808782324,19.3761004173277,0.301060933840606));
#181747=CARTESIAN_POINT('Ctrl Pts',(20.8489855761766,19.3033309946067,0.305428858049198));
#181748=CARTESIAN_POINT('Ctrl Pts',(20.8521613682029,19.2305845202816,0.309795404799371));
#181749=CARTESIAN_POINT('Ctrl Pts',(20.8515806736046,19.1576486643711,0.314161951549544));
#181750=CARTESIAN_POINT('Ctrl Pts',(20.8472434850165,19.0849405971963,0.318528498299718));
#181751=CARTESIAN_POINT('Ctrl Pts',(20.842906223341,19.0122313047933,0.322895118632042));
#181752=CARTESIAN_POINT('Ctrl Pts',(20.8348123728149,18.9397502915731,0.327261738964367));
#181753=CARTESIAN_POINT('Ctrl Pts',(20.823013932432,18.8679113961305,0.331628359296692));
#181754=CARTESIAN_POINT('Ctrl Pts',(20.8112032798744,18.7959981426281,0.335999499372999));
#181755=CARTESIAN_POINT('Ctrl Pts',(20.7956804601328,18.7247288123435,0.340370639449306));
#181756=CARTESIAN_POINT('Ctrl Pts',(20.7765488036571,18.6545079653052,0.344741779525613));
#181757=CARTESIAN_POINT('Ctrl Pts',(20.7574067702789,18.5842490308755,0.349115290483644));
#181758=CARTESIAN_POINT('Ctrl Pts',(20.7346521545123,18.5150401717767,0.353488801441674));
#181759=CARTESIAN_POINT('Ctrl Pts',(20.7084376488589,18.4472690455608,0.357862312399705));
#181760=CARTESIAN_POINT('Ctrl Pts',(20.6821764073163,18.3793770952528,0.362243620564604));
#181761=CARTESIAN_POINT('Ctrl Pts',(20.6524431558452,18.3129284384101,0.366624928729503));
#181762=CARTESIAN_POINT('Ctrl Pts',(20.6194377827199,18.2482885336239,0.371006236894402));
#181763=CARTESIAN_POINT('Ctrl Pts',(20.5965703635706,18.2035034681465,0.37404177931499));
#181764=CARTESIAN_POINT('Ctrl Pts',(20.572133215651,18.1595861430692,0.377077321735578));
#181765=CARTESIAN_POINT('Ctrl Pts',(20.54620485702,18.1166497104705,0.380112864156166));
#181766=CARTESIAN_POINT('Ctrl Pts',(20.5087129403854,18.0545644402657,0.384502201136291));
#181767=CARTESIAN_POINT('Ctrl Pts',(20.4679538797132,17.9942872987423,0.388891538116417));
#181768=CARTESIAN_POINT('Ctrl Pts',(20.4241274618398,17.9361830865827,0.393280875096542));
#181769=CARTESIAN_POINT('Ctrl Pts',(20.3803660305828,17.8781650324147,0.397663703487275));
#181770=CARTESIAN_POINT('Ctrl Pts',(20.3335465592593,17.8223138929919,0.402046531878009));
#181771=CARTESIAN_POINT('Ctrl Pts',(20.2839133009207,17.7689674900928,0.406429360268742));
#181772=CARTESIAN_POINT('Ctrl Pts',(20.2343383423802,17.7156837484944,0.410807040538659));
#181773=CARTESIAN_POINT('Ctrl Pts',(20.1819564893205,17.6648992500389,0.415184720808577));
#181774=CARTESIAN_POINT('Ctrl Pts',(20.127052568789,17.6169192176711,0.419562401078494));
#181775=CARTESIAN_POINT('Ctrl Pts',(20.0721834605649,17.5689696074593,0.423937305642237));
#181776=CARTESIAN_POINT('Ctrl Pts',(20.0147958199512,17.5238212515477,0.42831221020598));
#181777=CARTESIAN_POINT('Ctrl Pts',(19.9552106611292,17.4817419159812,0.432687114769722));
#181778=CARTESIAN_POINT('Ctrl Pts',(19.8956436547537,17.4396753997627,0.437060686531428));
#181779=CARTESIAN_POINT('Ctrl Pts',(19.8338808528526,17.4006763255857,0.441434258293133));
#181780=CARTESIAN_POINT('Ctrl Pts',(19.7702742782372,17.3649705797946,0.445807830054838));
#181781=CARTESIAN_POINT('Ctrl Pts',(19.7066661290221,17.3292639500971,0.450181510085618));
#181782=CARTESIAN_POINT('Ctrl Pts',(19.6412145378354,17.2968510448943,0.454555190116397));
#181783=CARTESIAN_POINT('Ctrl Pts',(19.5742968108293,17.2679121816783,0.458928870147177));
#181784=CARTESIAN_POINT('Ctrl Pts',(19.5073098565464,17.2389433808242,0.463307074807999));
#181785=CARTESIAN_POINT('Ctrl Pts',(19.438854181596,17.2134559893026,0.46768527946882));
#181786=CARTESIAN_POINT('Ctrl Pts',(19.3693270226857,17.191582119955,0.472063484129642));
#181787=CARTESIAN_POINT('Ctrl Pts',(19.2997619936055,17.1696963363115,0.476444073518355));
#181788=CARTESIAN_POINT('Ctrl Pts',(19.2291247856184,17.1514281144628,0.480824662907068));
#181789=CARTESIAN_POINT('Ctrl Pts',(19.1578251136209,17.1368589071463,0.485205252295781));
#181790=CARTESIAN_POINT('Ctrl Pts',(19.0863994489355,17.1222639547802,0.489593582564874));
#181791=CARTESIAN_POINT('Ctrl Pts',(19.0143094596386,17.1113811421464,0.493981912833966));
#181792=CARTESIAN_POINT('Ctrl Pts',(18.9419717193456,17.1042402215838,0.498370243103058));
#181793=CARTESIAN_POINT('Ctrl Pts',(18.8929675902332,17.0994027108761,0.501343052347906));
#181794=CARTESIAN_POINT('Ctrl Pts',(18.8438498553954,17.0962813345305,0.504315861592753));
#181795=CARTESIAN_POINT('Ctrl Pts',(18.7947475345845,17.0948717578932,0.5072886708376));
#181796=CARTESIAN_POINT('Ctrl Pts',(18.7222522737112,17.0927906418817,0.511677762395247));
#181797=CARTESIAN_POINT('Ctrl Pts',(18.6495091103978,17.0944351532161,0.516066853952895));
#181798=CARTESIAN_POINT('Ctrl Pts',(18.5769329023863,17.0998346993077,0.520455945510542));
#181799=CARTESIAN_POINT('Ctrl Pts',(18.5044640605617,17.1052262575382,0.524838544030911));
#181800=CARTESIAN_POINT('Ctrl Pts',(18.4321621606072,17.1143617873598,0.52922114255128));
#181801=CARTESIAN_POINT('Ctrl Pts',(18.3604434342997,17.1272187033611,0.533603741071649));
#181802=CARTESIAN_POINT('Ctrl Pts',(18.2888085527942,17.1400605886216,0.537981215991468));
#181803=CARTESIAN_POINT('Ctrl Pts',(18.2177559628243,17.1566151328627,0.542358690911286));
#181804=CARTESIAN_POINT('Ctrl Pts',(18.1476964397083,17.1768079895965,0.546736165831104));
#181805=CARTESIAN_POINT('Ctrl Pts',(18.0776810968814,17.1969881124977,0.551110880268136));
#181806=CARTESIAN_POINT('Ctrl Pts',(18.0086580405141,17.2208018623067,0.555485594705167));
#181807=CARTESIAN_POINT('Ctrl Pts',(17.9410261268035,17.2481241923067,0.559860309142198));
#181808=CARTESIAN_POINT('Ctrl Pts',(17.8734145775146,17.2754382953703,0.564233706323447));
#181809=CARTESIAN_POINT('Ctrl Pts',(17.8071937860416,17.3062587006989,0.568607103504695));
#181810=CARTESIAN_POINT('Ctrl Pts',(17.742744167297,17.340411623544,0.572980500685944));
#181811=CARTESIAN_POINT('Ctrl Pts',(17.6782927189291,17.3745655159369,0.577354022021053));
#181812=CARTESIAN_POINT('Ctrl Pts',(17.6156129682129,17.4120518861517,0.581727543356163));
#181813=CARTESIAN_POINT('Ctrl Pts',(17.5550606878344,17.4526510305885,0.586101064691273));
#181814=CARTESIAN_POINT('Ctrl Pts',(17.4944454063011,17.4932924160932,0.590479136423054));
#181815=CARTESIAN_POINT('Ctrl Pts',(17.435962415829,17.5370527729163,0.594857208154836));
#181816=CARTESIAN_POINT('Ctrl Pts',(17.3799377355334,17.5836695529341,0.599235279886618));
#181817=CARTESIAN_POINT('Ctrl Pts',(17.3238823567117,17.6303118764522,0.603615750567371));
#181818=CARTESIAN_POINT('Ctrl Pts',(17.2702883244171,17.6798134120468,0.607996221248125));
#181819=CARTESIAN_POINT('Ctrl Pts',(17.2194458037231,17.7318737083873,0.612376691928879));
#181820=CARTESIAN_POINT('Ctrl Pts',(17.1685131538602,17.7840262926627,0.616764927924508));
#181821=CARTESIAN_POINT('Ctrl Pts',(17.1203420749117,17.8387463335722,0.621153163920138));
#181822=CARTESIAN_POINT('Ctrl Pts',(17.0751829640465,17.895699638398,0.625541399915768));
#181823=CARTESIAN_POINT('Ctrl Pts',(17.0445739865328,17.9343027550967,0.628515759116856));
#181824=CARTESIAN_POINT('Ctrl Pts',(17.0153478916349,17.9739312043245,0.631490118317945));
#181825=CARTESIAN_POINT('Ctrl Pts',(16.9875709408017,18.0144739696991,0.634464477519034));
#181826=CARTESIAN_POINT('Ctrl Pts',(16.9460128011877,18.0751315240105,0.638914528054931));
#181827=CARTESIAN_POINT('Ctrl Pts',(16.907540976001,18.1380696073307,0.643364578590828));
#181828=CARTESIAN_POINT('Ctrl Pts',(16.8724100479184,18.2029465042425,0.647814629126725));
#181829=CARTESIAN_POINT('Ctrl Pts',(16.8373354125813,18.2677194443605,0.652257549035117));
#181830=CARTESIAN_POINT('Ctrl Pts',(16.8055912619724,18.3344246233501,0.656700468943509));
#181831=CARTESIAN_POINT('Ctrl Pts',(16.7773892640252,18.4026910071835,0.6611433888519));
#181832=CARTESIAN_POINT('Ctrl Pts',(16.7492305714797,18.4708525649974,0.665579486462369));
#181833=CARTESIAN_POINT('Ctrl Pts',(16.7246033918711,18.5405701336241,0.670015584072838));
#181834=CARTESIAN_POINT('Ctrl Pts',(16.7036729534574,18.6114492648012,0.674451681683307));
#181835=CARTESIAN_POINT('Ctrl Pts',(16.6827615040683,18.6822640912779,0.67888375466872));
#181836=CARTESIAN_POINT('Ctrl Pts',(16.6655402658946,18.7542379435046,0.683315827654133));
#181837=CARTESIAN_POINT('Ctrl Pts',(16.6521255559742,18.8269585968775,0.687747900639545));
#181838=CARTESIAN_POINT('Ctrl Pts',(16.6387183882743,18.8996383641481,0.69217748175805));
#181839=CARTESIAN_POINT('Ctrl Pts',(16.6291135834743,18.9730636427319,0.696607062876554));
#181840=CARTESIAN_POINT('Ctrl Pts',(16.6233766644396,19.0468106721261,0.701036643995058));
#181841=CARTESIAN_POINT('Ctrl Pts',(16.6190996536644,19.1017908518083,0.704339002989208));
#181842=CARTESIAN_POINT('Ctrl Pts',(16.6169713924502,19.1569495703029,0.707641361983357));
#181843=CARTESIAN_POINT('Ctrl Pts',(16.6170002905278,19.2121090962233,0.710943720977507));
#181844=CARTESIAN_POINT('',(20.3539256943887,20.5739122292573,0.));
#181845=CARTESIAN_POINT('Origin',(18.734,19.211,0.));
#181846=CARTESIAN_POINT('',(16.617000615792,19.2126147021618,0.489056278967189));
#181847=CARTESIAN_POINT('Ctrl Pts',(16.617000615792,19.2126147021618,0.489056278967189));
#181848=CARTESIAN_POINT('Ctrl Pts',(16.6169439872409,19.1383702930775,0.484575909845402));
#181849=CARTESIAN_POINT('Ctrl Pts',(16.620797922571,19.0639813997485,0.480095540723615));
#181850=CARTESIAN_POINT('Ctrl Pts',(16.6285774658501,18.9899005818784,0.475615171601828));
#181851=CARTESIAN_POINT('Ctrl Pts',(16.6360763305565,18.9184925299366,0.471296449965575));
#181852=CARTESIAN_POINT('Ctrl Pts',(16.6472223423582,18.847371251054,0.466977728329323));
#181853=CARTESIAN_POINT('Ctrl Pts',(16.6619760571586,18.7769426532218,0.46265900669307));
#181854=CARTESIAN_POINT('Ctrl Pts',(16.6767199431811,18.7065609742206,0.458343162146202));
#181855=CARTESIAN_POINT('Ctrl Pts',(16.6950666659526,18.6368715461706,0.454027317599334));
#181856=CARTESIAN_POINT('Ctrl Pts',(16.7169252821381,18.568272544104,0.449711473052466));
#181857=CARTESIAN_POINT('Ctrl Pts',(16.7387770072278,18.4996951683974,0.445396989108594));
#181858=CARTESIAN_POINT('Ctrl Pts',(16.7641382782578,18.4322080094981,0.441082505164722));
#181859=CARTESIAN_POINT('Ctrl Pts',(16.7928681313892,18.3661946563476,0.43676802122085));
#181860=CARTESIAN_POINT('Ctrl Pts',(16.8215990088179,18.300178949642,0.432453383453916));
#181861=CARTESIAN_POINT('Ctrl Pts',(16.8536985054739,18.235637607015,0.428138745686983));
#181862=CARTESIAN_POINT('Ctrl Pts',(16.8889780484646,18.1729330472689,0.423824107920049));
#181863=CARTESIAN_POINT('Ctrl Pts',(16.9242924797719,18.1101664783144,0.419505203361778));
#181864=CARTESIAN_POINT('Ctrl Pts',(16.9627929858512,18.0492407485845,0.415186298803507));
#181865=CARTESIAN_POINT('Ctrl Pts',(17.0042462481892,17.9904915165816,0.410867394245236));
#181866=CARTESIAN_POINT('Ctrl Pts',(17.0457241655954,17.9317073424234,0.406545920941331));
#181867=CARTESIAN_POINT('Ctrl Pts',(17.0901580238556,17.8751026293948,0.402224447637425));
#181868=CARTESIAN_POINT('Ctrl Pts',(17.1372743354942,17.8209798014746,0.39790297433352));
#181869=CARTESIAN_POINT('Ctrl Pts',(17.1844652352621,17.7667712936627,0.393574659861494));
#181870=CARTESIAN_POINT('Ctrl Pts',(17.2343467107437,17.7150528602031,0.389246345389468));
#181871=CARTESIAN_POINT('Ctrl Pts',(17.2866094106097,17.6660891670571,0.384918030917442));
#181872=CARTESIAN_POINT('Ctrl Pts',(17.3002561761556,17.6533038336867,0.383787827293062));
#181873=CARTESIAN_POINT('Ctrl Pts',(17.314065135147,17.64070610536,0.382657623668683));
#181874=CARTESIAN_POINT('Ctrl Pts',(17.3280304443276,17.6283002152896,0.381527420044303));
#181875=CARTESIAN_POINT('Ctrl Pts',(17.3823195172276,17.5800732650869,0.377133839768919));
#181876=CARTESIAN_POINT('Ctrl Pts',(17.4391958858,17.5345513015008,0.372740259493535));
#181877=CARTESIAN_POINT('Ctrl Pts',(17.4983592346194,17.4920232988985,0.368346679218151));
#181878=CARTESIAN_POINT('Ctrl Pts',(17.5574362854365,17.4495573293242,0.363959507592861));
#181879=CARTESIAN_POINT('Ctrl Pts',(17.6187933062775,17.4100769290324,0.359572335967571));
#181880=CARTESIAN_POINT('Ctrl Pts',(17.6820956267705,17.3738320192261,0.35518516434228));
#181881=CARTESIAN_POINT('Ctrl Pts',(17.7453254808101,17.3376286014228,0.350803015009472));
#181882=CARTESIAN_POINT('Ctrl Pts',(17.8104957951169,17.304653553715,0.346420865676663));
#181883=CARTESIAN_POINT('Ctrl Pts',(17.877242918952,17.2751135611627,0.342038716343855));
#181884=CARTESIAN_POINT('Ctrl Pts',(17.9439489018954,17.245591776161,0.337659268034266));
#181885=CARTESIAN_POINT('Ctrl Pts',(18.0122293270667,17.2195010391259,0.333279819724678));
#181886=CARTESIAN_POINT('Ctrl Pts',(18.0816971982504,17.1970014759614,0.328900371415089));
#181887=CARTESIAN_POINT('Ctrl Pts',(18.151144994395,17.1745084147899,0.324522188691947));
#181888=CARTESIAN_POINT('Ctrl Pts',(18.2217790979678,17.155604615017,0.320144005968805));
#181889=CARTESIAN_POINT('Ctrl Pts',(18.2931954157568,17.1404009759226,0.315765823245664));
#181890=CARTESIAN_POINT('Ctrl Pts',(18.3646144753839,17.1251967531253,0.311387472433939));
#181891=CARTESIAN_POINT('Ctrl Pts',(18.4368153380914,17.113693071257,0.307009121622214));
#181892=CARTESIAN_POINT('Ctrl Pts',(18.5093833633923,17.1059497947652,0.302630770810489));
#181893=CARTESIAN_POINT('Ctrl Pts',(18.5820273386456,17.0981984141328,0.298247837601298));
#181894=CARTESIAN_POINT('Ctrl Pts',(18.6550387645183,17.09421534768,0.293864904392108));
#181895=CARTESIAN_POINT('Ctrl Pts',(18.7279983301932,17.0940085073483,0.289481971182917));
#181896=CARTESIAN_POINT('Ctrl Pts',(18.8009982495664,17.093801552614,0.285096613787635));
#181897=CARTESIAN_POINT('Ctrl Pts',(18.8739457709895,17.0973749591399,0.280711256392353));
#181898=CARTESIAN_POINT('Ctrl Pts',(18.9464247464519,17.1046845613501,0.276325898997071));
#181899=CARTESIAN_POINT('Ctrl Pts',(19.0190318084557,17.1120070812604,0.271932791695594));
#181900=CARTESIAN_POINT('Ctrl Pts',(19.0911681952095,17.1230789093043,0.267539684394118));
#181901=CARTESIAN_POINT('Ctrl Pts',(19.1624265854904,17.1378044807966,0.263146577092641));
#181902=CARTESIAN_POINT('Ctrl Pts',(19.209979484077,17.1476313040667,0.26021492251605));
#181903=CARTESIAN_POINT('Ctrl Pts',(19.2571416240955,17.1590841897826,0.25728326793946));
#181904=CARTESIAN_POINT('Ctrl Pts',(19.3037962299318,17.1721225499419,0.254351613362869));
#181905=CARTESIAN_POINT('Ctrl Pts',(19.3728933426701,17.1914328200792,0.250009729787665));
#181906=CARTESIAN_POINT('Ctrl Pts',(19.441158849408,17.2143020129624,0.245667846212462));
#181907=CARTESIAN_POINT('Ctrl Pts',(19.5081940657064,17.2406415177372,0.241325962637258));
#181908=CARTESIAN_POINT('Ctrl Pts',(19.575128336692,17.2669413590381,0.236990617308954));
#181909=CARTESIAN_POINT('Ctrl Pts',(19.6408355376982,17.2967009666761,0.232655271980649));
#181910=CARTESIAN_POINT('Ctrl Pts',(19.7049304637962,17.3297815027296,0.228319926652345));
#181911=CARTESIAN_POINT('Ctrl Pts',(19.7689517228447,17.3628240179031,0.223989564122503));
#181912=CARTESIAN_POINT('Ctrl Pts',(19.8313639491299,17.3991796603212,0.219659201592662));
#181913=CARTESIAN_POINT('Ctrl Pts',(19.8918020078126,17.4386615699294,0.21532883906282));
#181914=CARTESIAN_POINT('Ctrl Pts',(19.9522029223966,17.4781192146956,0.211001137892668));
#181915=CARTESIAN_POINT('Ctrl Pts',(20.0106316627094,17.5206990484192,0.206673436722516));
#181916=CARTESIAN_POINT('Ctrl Pts',(20.0667492121328,17.5661691462161,0.202345735552364));
#181917=CARTESIAN_POINT('Ctrl Pts',(20.1228517146943,17.6116270520643,0.198019194773624));
#181918=CARTESIAN_POINT('Ctrl Pts',(20.1766438725233,17.6599733741804,0.193692653994883));
#181919=CARTESIAN_POINT('Ctrl Pts',(20.2278185824314,17.710934987148,0.189366113216143));
#181920=CARTESIAN_POINT('Ctrl Pts',(20.2789973003963,17.7619005914824,0.185039233578198));
#181921=CARTESIAN_POINT('Ctrl Pts',(20.3275578154845,17.8154815434691,0.180712353940253));
#181922=CARTESIAN_POINT('Ctrl Pts',(20.3732301490776,17.8713681407361,0.176385474302308));
#181923=CARTESIAN_POINT('Ctrl Pts',(20.4189572946786,17.9273218082918,0.172053401915454));
#181924=CARTESIAN_POINT('Ctrl Pts',(20.4617890269818,17.9855862615223,0.167721329528601));
#181925=CARTESIAN_POINT('Ctrl Pts',(20.5014965046459,18.0458197109183,0.163389257141747));
#181926=CARTESIAN_POINT('Ctrl Pts',(20.5412284893311,18.1060903357408,0.159054511047183));
#181927=CARTESIAN_POINT('Ctrl Pts',(20.5778321351825,18.1683319477764,0.154719764952619));
#181928=CARTESIAN_POINT('Ctrl Pts',(20.6111242325247,18.2321774340216,0.150385018858055));
#181929=CARTESIAN_POINT('Ctrl Pts',(20.6444833803135,18.2961515053878,0.146041542563685));
#181930=CARTESIAN_POINT('Ctrl Pts',(20.6745174591996,18.3617354510943,0.141698066269316));
#181931=CARTESIAN_POINT('Ctrl Pts',(20.7010913635959,18.4285419709235,0.137354589974947));
#181932=CARTESIAN_POINT('Ctrl Pts',(20.7218496990689,18.480728210842,0.133961662210443));
#181933=CARTESIAN_POINT('Ctrl Pts',(20.7404975995388,18.5336600360754,0.130568734445939));
#181934=CARTESIAN_POINT('Ctrl Pts',(20.7569922795081,18.5871480648016,0.127175806681435));
#181935=CARTESIAN_POINT('Ctrl Pts',(20.7789195363731,18.6582525510522,0.12266540704014));
#181936=CARTESIAN_POINT('Ctrl Pts',(20.7971288498248,18.7306277670711,0.118155007398845));
#181937=CARTESIAN_POINT('Ctrl Pts',(20.8114809457081,18.8038613010046,0.113644607757551));
#181938=CARTESIAN_POINT('Ctrl Pts',(20.8265483310552,18.8807446973446,0.108909415767653));
#181939=CARTESIAN_POINT('Ctrl Pts',(20.8373637791173,18.9585737514705,0.104174223777755));
#181940=CARTESIAN_POINT('Ctrl Pts',(20.8438249692462,19.0368517897157,0.0994390317878569));
#181941=CARTESIAN_POINT('Ctrl Pts',(20.8499589678183,19.1111658657987,0.0949436276401115));
#181942=CARTESIAN_POINT('Ctrl Pts',(20.8521688918293,19.1858840436361,0.0904482234923663));
#181943=CARTESIAN_POINT('Ctrl Pts',(20.8504195410052,19.2605714277716,0.0859528193446209));
#181944=CARTESIAN_POINT('Ctrl Pts',(20.8486718350827,19.3351885839162,0.0814616421919066));
#181945=CARTESIAN_POINT('Ctrl Pts',(20.8429722647592,19.4097745558195,0.0769704650391922));
#181946=CARTESIAN_POINT('Ctrl Pts',(20.8333376405566,19.4838927828696,0.0724792878864778));
#181947=CARTESIAN_POINT('Ctrl Pts',(20.8237095586262,19.5579606808563,0.0679911604119481));
#181948=CARTESIAN_POINT('Ctrl Pts',(20.8101517936905,19.6315610202815,0.0635030329374184));
#181949=CARTESIAN_POINT('Ctrl Pts',(20.7927330149949,19.7042619719479,0.0590149054628886));
#181950=CARTESIAN_POINT('Ctrl Pts',(20.7753215178591,19.7769325324869,0.0545286541571083));
#181951=CARTESIAN_POINT('Ctrl Pts',(20.7540523227982,19.8487040161605,0.0500424028513279));
#181952=CARTESIAN_POINT('Ctrl Pts',(20.7290450048267,19.919155652887,0.0455561515455476));
#181953=CARTESIAN_POINT('Ctrl Pts',(20.704034580516,19.9896160409194,0.0410693429701386));
#181954=CARTESIAN_POINT('Ctrl Pts',(20.6752852491506,20.0587558278079,0.0365825343947297));
#181955=CARTESIAN_POINT('Ctrl Pts',(20.642965902348,20.1261711226173,0.0320957258193207));
#181956=CARTESIAN_POINT('Ctrl Pts',(20.6106450021441,20.1935896576844,0.0276087015893536));
#181957=CARTESIAN_POINT('Ctrl Pts',(20.5747539463686,20.2592831330904,0.0231216773593865));
#181958=CARTESIAN_POINT('Ctrl Pts',(20.5355083127276,20.3228708554384,0.0186346531294194));
#181959=CARTESIAN_POINT('Ctrl Pts',(20.4962355967949,20.3865024578589,0.0141445325320924));
#181960=CARTESIAN_POINT('Ctrl Pts',(20.4536039241545,20.448025026832,0.00965441193476544));
#181961=CARTESIAN_POINT('Ctrl Pts',(20.4078726283013,20.5070861947508,0.00516429133743847));
#181962=CARTESIAN_POINT('Ctrl Pts',(20.390340082504,20.5297291706837,0.00344286089162564));
#181963=CARTESIAN_POINT('Ctrl Pts',(20.3723523809939,20.5520106992443,0.00172143044581282));
#181964=CARTESIAN_POINT('Ctrl Pts',(20.3539256943887,20.5739122292573,0.));
#181965=CARTESIAN_POINT('Ctrl Pts',(16.617000568856,19.2125519458626,0.490010468414518));
#181966=CARTESIAN_POINT('Ctrl Pts',(16.6170514727118,19.2819895701466,0.494577329568179));
#181967=CARTESIAN_POINT('Ctrl Pts',(16.620518701297,19.351389617805,0.499098993300903));
#181968=CARTESIAN_POINT('Ctrl Pts',(16.6297024930679,19.4437365273411,0.504962251941776));
#181969=CARTESIAN_POINT('Ctrl Pts',(16.6323977852857,19.4669346043809,0.506421959053868));
#181970=CARTESIAN_POINT('Ctrl Pts',(16.6362852638933,19.4961657824342,0.50824070320294));
#181971=CARTESIAN_POINT('Ctrl Pts',(16.6371204772031,19.5022437235427,0.508617740340019));
#181972=CARTESIAN_POINT('Ctrl Pts',(16.6385603510653,19.5123944747752,0.509245445913265));
#181973=CARTESIAN_POINT('Ctrl Pts',(16.6391504869417,19.5164692620273,0.509496889213504));
#181974=CARTESIAN_POINT('Ctrl Pts',(16.6402462304663,19.5238826521267,0.509953342278766));
#181975=CARTESIAN_POINT('Ctrl Pts',(16.6407479434933,19.5272218046519,0.510158566898216));
#181976=CARTESIAN_POINT('Ctrl Pts',(16.6417945776025,19.5340760326796,0.510579044653468));
#181977=CARTESIAN_POINT('Ctrl Pts',(16.642340366501,19.5375909222486,0.51079424148904));
#181978=CARTESIAN_POINT('Ctrl Pts',(16.6435932942979,19.5455278134933,0.51127920871026));
#181979=CARTESIAN_POINT('Ctrl Pts',(16.6443056041383,19.5499489430603,0.511548681784669));
#181980=CARTESIAN_POINT('Ctrl Pts',(16.6465009500227,19.5633049044377,0.512360805496415));
#181981=CARTESIAN_POINT('Ctrl Pts',(16.6480273223423,19.5722326453654,0.512901042489817));
#181982=CARTESIAN_POINT('Ctrl Pts',(16.6601811269454,19.6406730694997,0.517024267613215));
#181983=CARTESIAN_POINT('Ctrl Pts',(16.6732971358806,19.6997216069459,0.52047584790657));
#181984=CARTESIAN_POINT('Ctrl Pts',(16.6938141846331,19.7764103007183,0.52491372259378));
#181985=CARTESIAN_POINT('Ctrl Pts',(16.6989489234585,19.7946215484647,0.525964177555541));
#181986=CARTESIAN_POINT('Ctrl Pts',(16.7159637149531,19.8520104643281,0.52927037703059));
#181987=CARTESIAN_POINT('Ctrl Pts',(16.7287365187921,19.8909142528046,0.531505687114406));
#181988=CARTESIAN_POINT('Ctrl Pts',(16.7435546041396,19.9319879022533,0.533880981460195));
#181989=CARTESIAN_POINT('Ctrl Pts',(16.7444845157121,19.9345499751618,0.534029210069973));
#181990=CARTESIAN_POINT('Ctrl Pts',(16.7454193623539,19.9371102172391,0.534177402122746));
#181991=CARTESIAN_POINT('Origin',(18.734,19.211,0.));
#181992=CARTESIAN_POINT('',(16.7454191763733,19.9371097078984,1.5557606494604));
#181993=CARTESIAN_POINT('',(16.7454193623274,19.9371102171666,1.33163196712539));
#181994=CARTESIAN_POINT('',(16.7454193623258,19.9371102171621,0.));
#181995=CARTESIAN_POINT('',(16.6170003908423,19.2122864004549,1.51094372094299));
#181996=CARTESIAN_POINT('Ctrl Pts',(16.7454191763733,19.9371097078984,1.5557606494604));
#181997=CARTESIAN_POINT('Ctrl Pts',(16.716143910019,19.8569341743039,1.55013146713003));
#181998=CARTESIAN_POINT('Ctrl Pts',(16.691724399299,19.7750071540623,1.54446139084034));
#181999=CARTESIAN_POINT('Ctrl Pts',(16.6660226724897,19.6647911110356,1.53708122705044));
#182000=CARTESIAN_POINT('Ctrl Pts',(16.6602607680098,19.6376875904994,1.53528609642957));
#182001=CARTESIAN_POINT('Ctrl Pts',(16.6468711285243,19.5680050736347,1.53073309112472));
#182002=CARTESIAN_POINT('Ctrl Pts',(16.6400127040676,19.5252886290076,1.52800093208224));
#182003=CARTESIAN_POINT('Ctrl Pts',(16.6335056814302,19.4749486682767,1.52487273165061));
#182004=CARTESIAN_POINT('Ctrl Pts',(16.6325834864648,19.4675032598284,1.52441240419798));
#182005=CARTESIAN_POINT('Ctrl Pts',(16.631157199937,19.4554637294837,1.52367198912816));
#182006=CARTESIAN_POINT('Ctrl Pts',(16.6306285480662,19.4508726598322,1.52339057211655));
#182007=CARTESIAN_POINT('Ctrl Pts',(16.6297175152803,19.4427261555249,1.52289290836678));
#182008=CARTESIAN_POINT('Ctrl Pts',(16.6293291048428,19.4391714495985,1.5226763260859));
#182009=CARTESIAN_POINT('Ctrl Pts',(16.6285936539188,19.4322789607038,1.52225749574951));
#182010=CARTESIAN_POINT('Ctrl Pts',(16.6282455446969,19.4289413565642,1.52205518625118));
#182011=CARTESIAN_POINT('Ctrl Pts',(16.6274962873484,19.4215882090119,1.52161055603733));
#182012=CARTESIAN_POINT('Ctrl Pts',(16.6270986810427,19.4175723068912,1.52136843279376));
#182013=CARTESIAN_POINT('Ctrl Pts',(16.6261439820916,19.4076400782142,1.52077130950579));
#182014=CARTESIAN_POINT('Ctrl Pts',(16.6256003084409,19.4017224556519,1.52041703549923));
#182015=CARTESIAN_POINT('Ctrl Pts',(16.6234160970895,19.3767968052736,1.51893078240055));
#182016=CARTESIAN_POINT('Ctrl Pts',(16.622007576511,19.3577686962519,1.51781083250504));
#182017=CARTESIAN_POINT('Ctrl Pts',(16.618313690624,19.2966545307416,1.51425336271375));
#182018=CARTESIAN_POINT('Ctrl Pts',(16.6170276587975,19.2545168990468,1.51186055981017));
#182019=CARTESIAN_POINT('Ctrl Pts',(16.6170004413594,19.2123670096225,1.50950271487047));
#182020=CARTESIAN_POINT('Ctrl Pts',(16.7454193623258,19.9371102171621,0.755484062589681));
#182021=CARTESIAN_POINT('Ctrl Pts',(16.7570609175801,19.9689926653415,0.757536136459943));
#182022=CARTESIAN_POINT('Ctrl Pts',(16.7694632428329,20.0005783913288,0.759588210330205));
#182023=CARTESIAN_POINT('Ctrl Pts',(16.7826102683356,20.0318331835122,0.761640284200467));
#182024=CARTESIAN_POINT('Ctrl Pts',(16.8107255683611,20.0986724742163,0.766028704419563));
#182025=CARTESIAN_POINT('Ctrl Pts',(16.8423337653793,20.1641959540946,0.770417124638659));
#182026=CARTESIAN_POINT('Ctrl Pts',(16.8772900666095,20.2280138756423,0.774805544857755));
#182027=CARTESIAN_POINT('Ctrl Pts',(16.9121945017389,20.291737107917,0.779187453797423));
#182028=CARTESIAN_POINT('Ctrl Pts',(16.950436949649,20.3537593859495,0.78356936273709));
#182029=CARTESIAN_POINT('Ctrl Pts',(16.9918247124447,20.4137112153097,0.787951271676757));
#182030=CARTESIAN_POINT('Ctrl Pts',(17.0331638556813,20.4735926172943,0.792328033044615));
#182031=CARTESIAN_POINT('Ctrl Pts',(17.0776407011702,20.5314080072912,0.796704794412473));
#182032=CARTESIAN_POINT('Ctrl Pts',(17.1250176841708,20.5868142706589,0.801081555780331));
#182033=CARTESIAN_POINT('Ctrl Pts',(17.1723646300877,20.6421854063664,0.805455542274424));
#182034=CARTESIAN_POINT('Ctrl Pts',(17.2226077526131,20.6951500803167,0.809829528768517));
#182035=CARTESIAN_POINT('Ctrl Pts',(17.2754682593319,20.7453970025596,0.81420351526261));
#182036=CARTESIAN_POINT('Ctrl Pts',(17.3283126854692,20.7956286392937,0.818576171155629));
#182037=CARTESIAN_POINT('Ctrl Pts',(17.3837725656567,20.8431438335996,0.822948827048648));
#182038=CARTESIAN_POINT('Ctrl Pts',(17.4415323658093,20.8876682482141,0.827321482941666));
#182039=CARTESIAN_POINT('Ctrl Pts',(17.4992936432934,20.9321938016366,0.831694250674801));
#182040=CARTESIAN_POINT('Ctrl Pts',(17.5593545743128,20.9737281306084,0.836067018407934));
#182041=CARTESIAN_POINT('Ctrl Pts',(17.6213680169052,21.0120383311286,0.840439786141068));
#182042=CARTESIAN_POINT('Ctrl Pts',(17.6834457957083,21.0503882767916,0.844817090427792));
#182043=CARTESIAN_POINT('Ctrl Pts',(17.7474797192073,21.0855071616625,0.849194394714516));
#182044=CARTESIAN_POINT('Ctrl Pts',(17.8130959539107,21.1172068979773,0.853571699001239));
#182045=CARTESIAN_POINT('Ctrl Pts',(17.8787480151553,21.1489239423855,0.857951393301242));
#182046=CARTESIAN_POINT('Ctrl Pts',(17.945983662843,21.1772179341103,0.862331087601244));
#182047=CARTESIAN_POINT('Ctrl Pts',(18.0144093958347,21.2019491109511,0.866710781901247));
#182048=CARTESIAN_POINT('Ctrl Pts',(18.0829563577891,21.2267241036896,0.87109823564749));
#182049=CARTESIAN_POINT('Ctrl Pts',(18.1526971536752,21.2479235359394,0.875485689393733));
#182050=CARTESIAN_POINT('Ctrl Pts',(18.2232240248379,21.2654578124647,0.879873143139976));
#182051=CARTESIAN_POINT('Ctrl Pts',(18.2711423361325,21.2773711854389,0.882854125720618));
#182052=CARTESIAN_POINT('Ctrl Pts',(18.3194232738606,21.2875936785606,0.885835108301261));
#182053=CARTESIAN_POINT('Ctrl Pts',(18.3679374539171,21.2961108393453,0.888816090881903));
#182054=CARTESIAN_POINT('Ctrl Pts',(18.4393551938946,21.3086489544605,0.893204396292285));
#182055=CARTESIAN_POINT('Ctrl Pts',(18.5115571780253,21.3175380608514,0.897592701702668));
#182056=CARTESIAN_POINT('Ctrl Pts',(18.5841373357919,21.3226889406057,0.90198100711305));
#182057=CARTESIAN_POINT('Ctrl Pts',(18.6566098149829,21.3278321786104,0.906362802114936));
#182058=CARTESIAN_POINT('Ctrl Pts',(18.7294588768749,21.3292481656289,0.910744597116822));
#182059=CARTESIAN_POINT('Ctrl Pts',(18.8022695496257,21.3268989268379,0.915126392118709));
#182060=CARTESIAN_POINT('Ctrl Pts',(18.8749947182522,21.3245524468404,0.919503041425181));
#182061=CARTESIAN_POINT('Ctrl Pts',(18.9476811075809,21.3184495401269,0.923879690731654));
#182062=CARTESIAN_POINT('Ctrl Pts',(19.0199116407238,21.3086042366706,0.928256340038127));
#182063=CARTESIAN_POINT('Ctrl Pts',(19.0920963984856,21.2987651725774,0.932630215686693));
#182064=CARTESIAN_POINT('Ctrl Pts',(19.163825396507,21.2851884825072,0.937004091335259));
#182065=CARTESIAN_POINT('Ctrl Pts',(19.2346860015942,21.2679400885314,0.941377966983825));
#182066=CARTESIAN_POINT('Ctrl Pts',(19.3055250721922,21.2506969363307,0.945750513414592));
#182067=CARTESIAN_POINT('Ctrl Pts',(19.3754958054007,21.2297844095034,0.950123059845359));
#182068=CARTESIAN_POINT('Ctrl Pts',(19.4441967521215,21.2053193258042,0.954495606276126));
#182069=CARTESIAN_POINT('Ctrl Pts',(19.5128994804463,21.1808536076582,0.95886826609902));
#182070=CARTESIAN_POINT('Ctrl Pts',(19.5803319031763,21.1528353134295,0.963240925921913));
#182071=CARTESIAN_POINT('Ctrl Pts',(19.6461103019391,21.1214302649133,0.967613585744807));
#182072=CARTESIAN_POINT('Ctrl Pts',(19.7119569921549,21.0899926115231,0.971990785284362));
#182073=CARTESIAN_POINT('Ctrl Pts',(19.7761457936512,21.0551613918966,0.976367984823917));
#182074=CARTESIAN_POINT('Ctrl Pts',(19.838316224423,21.0171491290799,0.980745184363471));
#182075=CARTESIAN_POINT('Ctrl Pts',(19.9005206239767,20.9791160970608,0.985124775524485));
#182076=CARTESIAN_POINT('Ctrl Pts',(19.960704058896,20.937898834125,0.989504366685498));
#182077=CARTESIAN_POINT('Ctrl Pts',(20.0185360368887,20.893752557548,0.993883957846511));
#182078=CARTESIAN_POINT('Ctrl Pts',(20.0764705271474,20.8495280278141,0.998271312217941));
#182079=CARTESIAN_POINT('Ctrl Pts',(20.1320448687351,20.8023644287408,1.00265866658937));
#182080=CARTESIAN_POINT('Ctrl Pts',(20.1849630355814,20.7525561194379,1.0070460209608));
#182081=CARTESIAN_POINT('Ctrl Pts',(20.2209299950565,20.7187028408952,1.01002797982831));
#182082=CARTESIAN_POINT('Ctrl Pts',(20.2556706870372,20.6836286165394,1.01300993869582));
#182083=CARTESIAN_POINT('Ctrl Pts',(20.2891028485224,20.6474345200939,1.01599189756334));
#182084=CARTESIAN_POINT('Ctrl Pts',(20.338299904051,20.59417314262,1.02037999541497));
#182085=CARTESIAN_POINT('Ctrl Pts',(20.3848536174481,20.5382773665806,1.02476809326661));
#182086=CARTESIAN_POINT('Ctrl Pts',(20.4284691674673,20.4800402832467,1.02915619111824));
#182087=CARTESIAN_POINT('Ctrl Pts',(20.4720199654849,20.421889659162,1.03353777436399));
#182088=CARTESIAN_POINT('Ctrl Pts',(20.5126409725289,20.3614050108817,1.03791935760974));
#182089=CARTESIAN_POINT('Ctrl Pts',(20.5500756321549,20.2989146557949,1.04230094085549));
#182090=CARTESIAN_POINT('Ctrl Pts',(20.5874662839342,20.2364977638033,1.04667737315167));
#182091=CARTESIAN_POINT('Ctrl Pts',(20.62167778275,20.1720802607426,1.05105380544786));
#182092=CARTESIAN_POINT('Ctrl Pts',(20.6524961574242,20.1060203874485,1.05543023774404));
#182093=CARTESIAN_POINT('Ctrl Pts',(20.6832949783004,20.0400024281564,1.05980389325936));
#182094=CARTESIAN_POINT('Ctrl Pts',(20.7107047431844,19.9723446023035,1.06417754877469));
#182095=CARTESIAN_POINT('Ctrl Pts',(20.7345575167902,19.9034295068915,1.06855120429001));
#182096=CARTESIAN_POINT('Ctrl Pts',(20.758403025892,19.8345353999817,1.07292352778254));
#182097=CARTESIAN_POINT('Ctrl Pts',(20.7786935367104,19.7643852393011,1.07729585127507));
#182098=CARTESIAN_POINT('Ctrl Pts',(20.7953099613678,19.6933797706848,1.0816681747676));
#182099=CARTESIAN_POINT('Ctrl Pts',(20.8119268074934,19.6223725010462,1.08604060916218));
#182100=CARTESIAN_POINT('Ctrl Pts',(20.8248692744613,19.550510350571,1.09041304355677));
#182101=CARTESIAN_POINT('Ctrl Pts',(20.8340690755323,19.4782056848069,1.09478547795135));
#182102=CARTESIAN_POINT('Ctrl Pts',(20.8432784235523,19.4058259860114,1.09916244977106));
#182103=CARTESIAN_POINT('Ctrl Pts',(20.8487372902008,19.3330033346485,1.10353942159077));
#182104=CARTESIAN_POINT('Ctrl Pts',(20.8504292342169,19.2601558394492,1.10791639341048));
#182105=CARTESIAN_POINT('Ctrl Pts',(20.8521221020959,19.1872685668714,1.1122957552158));
#182106=CARTESIAN_POINT('Ctrl Pts',(20.8500439658808,19.1143569059928,1.11667511702111));
#182107=CARTESIAN_POINT('Ctrl Pts',(20.844230516392,19.041836860729,1.12105447882643));
#182108=CARTESIAN_POINT('Ctrl Pts',(20.8384067616499,18.9691882622835,1.12544160373905));
#182109=CARTESIAN_POINT('Ctrl Pts',(20.8288345343212,18.8969331443913,1.12982872865168));
#182110=CARTESIAN_POINT('Ctrl Pts',(20.815601093585,18.8254797188399,1.1342158535643));
#182111=CARTESIAN_POINT('Ctrl Pts',(20.8066002264401,18.7768799024162,1.13719980379112));
#182112=CARTESIAN_POINT('Ctrl Pts',(20.7959066867639,18.728650750081,1.14018375401795));
#182113=CARTESIAN_POINT('Ctrl Pts',(20.7835610201373,18.6809163983542,1.14316770424477));
#182114=CARTESIAN_POINT('Ctrl Pts',(20.7654052835722,18.6107174904079,1.14755594960082));
#182115=CARTESIAN_POINT('Ctrl Pts',(20.7436033968818,18.5413154230199,1.15194419495686));
#182116=CARTESIAN_POINT('Ctrl Pts',(20.7182422538736,18.4731167585976,1.15633244031291));
#182117=CARTESIAN_POINT('Ctrl Pts',(20.692918748692,18.4050193060766,1.16071417318576));
#182118=CARTESIAN_POINT('Ctrl Pts',(20.6640466398308,18.3381221595675,1.16509590605861));
#182119=CARTESIAN_POINT('Ctrl Pts',(20.6317631518085,18.2728187703658,1.16947763893146));
#182120=CARTESIAN_POINT('Ctrl Pts',(20.5995175966481,18.207592112168,1.17385422330028));
#182121=CARTESIAN_POINT('Ctrl Pts',(20.5638688376431,18.1439559215066,1.1782308076691));
#182122=CARTESIAN_POINT('Ctrl Pts',(20.5250023096655,18.0822840362727,1.18260739203792));
#182123=CARTESIAN_POINT('Ctrl Pts',(20.486160428393,18.0206512594659,1.18698120105247));
#182124=CARTESIAN_POINT('Ctrl Pts',(20.4441050833308,17.9609807236605,1.19135501006701));
#182125=CARTESIAN_POINT('Ctrl Pts',(20.3990671060294,17.9036207388754,1.19572881908156));
#182126=CARTESIAN_POINT('Ctrl Pts',(20.3540428324429,17.8462782070248,1.20010129727632));
#182127=CARTESIAN_POINT('Ctrl Pts',(20.3060380260511,17.7912452096239,1.20447377547108));
#182128=CARTESIAN_POINT('Ctrl Pts',(20.2553252174912,17.7388388054886,1.20884625366584));
#182129=CARTESIAN_POINT('Ctrl Pts',(20.2046111112934,17.6864310603796,1.21321884374345));
#182130=CARTESIAN_POINT('Ctrl Pts',(20.15118920223,17.6366503872243,1.21759143382106));
#182131=CARTESIAN_POINT('Ctrl Pts',(20.0953692876952,17.589777417342,1.22196402389866));
#182132=CARTESIAN_POINT('Ctrl Pts',(20.0394914434218,17.5428558028332,1.22634115183705));
#182133=CARTESIAN_POINT('Ctrl Pts',(19.9812109951272,17.4988482273088,1.23071827977543));
#182134=CARTESIAN_POINT('Ctrl Pts',(19.9208706311964,17.4579948360591,1.23509540771381));
#182135=CARTESIAN_POINT('Ctrl Pts',(19.8604973137098,17.4171191336329,1.23947492612385));
#182136=CARTESIAN_POINT('Ctrl Pts',(19.798062253929,17.3794012947369,1.2438544445339));
#182137=CARTESIAN_POINT('Ctrl Pts',(19.7339345878002,17.3450364901422,1.24823396294394));
#182138=CARTESIAN_POINT('Ctrl Pts',(19.6696932633544,17.310610778203,1.25262124350598));
#182139=CARTESIAN_POINT('Ctrl Pts',(19.6037537785759,17.2795501739061,1.25700852406801));
#182140=CARTESIAN_POINT('Ctrl Pts',(19.5365066298311,17.2520022692517,1.26139580463005));
#182141=CARTESIAN_POINT('Ctrl Pts',(19.4907905552443,17.2332746044005,1.26437837339544));
#182142=CARTESIAN_POINT('Ctrl Pts',(19.4444705346851,17.2161693425274,1.26736094216082));
#182143=CARTESIAN_POINT('Ctrl Pts',(19.3976727118507,17.200719539083,1.27034351092621));
#182144=CARTESIAN_POINT('Ctrl Pts',(19.3288196249543,17.1779884247991,1.27473172930774));
#182145=CARTESIAN_POINT('Ctrl Pts',(19.2586629673008,17.1587544123363,1.27911994768926));
#182146=CARTESIAN_POINT('Ctrl Pts',(19.1875916222504,17.1431645035873,1.28350816607079));
#182147=CARTESIAN_POINT('Ctrl Pts',(19.116625754035,17.1275977317894,1.28788987190657));
#182148=CARTESIAN_POINT('Ctrl Pts',(19.0447483604959,17.1156644301751,1.29227157774234));
#182149=CARTESIAN_POINT('Ctrl Pts',(18.9723645440813,17.1074621838139,1.29665328357812));
#182150=CARTESIAN_POINT('Ctrl Pts',(18.9000657779753,17.0992695750156,1.30102984095045));
#182151=CARTESIAN_POINT('Ctrl Pts',(18.8272622479781,17.0947993667585,1.30540639832278));
#182152=CARTESIAN_POINT('Ctrl Pts',(18.7543686604617,17.0940979905364,1.3097829556951));
#182153=CARTESIAN_POINT('Ctrl Pts',(18.6815212970999,17.0933970590794,1.31415673775246));
#182154=CARTESIAN_POINT('Ctrl Pts',(18.6085844706957,17.0964602223415,1.31853051980982));
#182155=CARTESIAN_POINT('Ctrl Pts',(18.535975995326,17.1032819226536,1.32290430186718));
#182156=CARTESIAN_POINT('Ctrl Pts',(18.4633896113716,17.1101015474364,1.32727675318408));
#182157=CARTESIAN_POINT('Ctrl Pts',(18.3911318600869,17.1206773938757,1.33164920450098));
#182158=CARTESIAN_POINT('Ctrl Pts',(18.3196168493103,17.1349519262733,1.33602165581788));
#182159=CARTESIAN_POINT('Ctrl Pts',(18.2481000066454,17.1492268243192,1.34039421913703));
#182160=CARTESIAN_POINT('Ctrl Pts',(18.1773264149147,17.1672005000461,1.34476678245618));
#182161=CARTESIAN_POINT('Ctrl Pts',(18.1076997240457,17.1887643647835,1.34913934577533));
#182162=CARTESIAN_POINT('Ctrl Pts',(18.0380007684381,17.2103506104072,1.35351644732747));
#182163=CARTESIAN_POINT('Ctrl Pts',(17.9694515520846,17.2355343416688,1.35789354887962));
#182164=CARTESIAN_POINT('Ctrl Pts',(17.9024394858624,17.2641573994472,1.36227065043177));
#182165=CARTESIAN_POINT('Ctrl Pts',(17.8353908196981,17.2927960902648,1.36665014262299));
#182166=CARTESIAN_POINT('Ctrl Pts',(17.7698814087054,17.3248776352815,1.37102963481421));
#182167=CARTESIAN_POINT('Ctrl Pts',(17.706275162751,17.3601972933612,1.37540912700542));
#182168=CARTESIAN_POINT('Ctrl Pts',(17.6425561737593,17.3955795560715,1.37979638191308));
#182169=CARTESIAN_POINT('Ctrl Pts',(17.5807474957366,17.4342111377127,1.38418363682075));
#182170=CARTESIAN_POINT('Ctrl Pts',(17.5211845942116,17.4758435829925,1.38857089172841));
#182171=CARTESIAN_POINT('Ctrl Pts',(17.4806889448312,17.5041486665888,1.39155370035482));
#182172=CARTESIAN_POINT('Ctrl Pts',(17.4412307383374,17.5338399733657,1.39453650898123));
#182173=CARTESIAN_POINT('Ctrl Pts',(17.4029060714275,17.5648293061418,1.39751931760764));
#182174=CARTESIAN_POINT('Ctrl Pts',(17.3472596997714,17.6098249725906,1.40185027442443));
#182175=CARTESIAN_POINT('Ctrl Pts',(17.2937750953766,17.6577445694628,1.40618123124122));
#182176=CARTESIAN_POINT('Ctrl Pts',(17.2427818430318,17.7083498716173,1.41051218805802));
#182177=CARTESIAN_POINT('Ctrl Pts',(17.1918753392824,17.7588690851488,1.41483577714667));
#182178=CARTESIAN_POINT('Ctrl Pts',(17.143452120906,17.8120645856498,1.41915936623532));
#182179=CARTESIAN_POINT('Ctrl Pts',(17.0978092703806,17.8676575655078,1.42348295532397));
#182180=CARTESIAN_POINT('Ctrl Pts',(17.0522098689332,17.9231976244002,1.427802428632));
#182181=CARTESIAN_POINT('Ctrl Pts',(17.0093859023338,17.9811302577511,1.43212190194003));
#182182=CARTESIAN_POINT('Ctrl Pts',(16.9695971044423,18.0411404263128,1.43644137524806));
#182183=CARTESIAN_POINT('Ctrl Pts',(16.929832242303,18.1011144945499,1.44075825008999));
#182184=CARTESIAN_POINT('Ctrl Pts',(16.8930992016319,18.1631632070369,1.44507512493191));
#182185=CARTESIAN_POINT('Ctrl Pts',(16.8596158064165,18.2269406040058,1.44939199977384));
#182186=CARTESIAN_POINT('Ctrl Pts',(16.826140825032,18.2907019747554,1.45370778985555));
#182187=CARTESIAN_POINT('Ctrl Pts',(16.795914098134,18.3561907283349,1.45802357993727));
#182188=CARTESIAN_POINT('Ctrl Pts',(16.7691077535852,18.4230358764645,1.46233937001898));
#182189=CARTESIAN_POINT('Ctrl Pts',(16.742282805863,18.4899274140556,1.46665815518985));
#182190=CARTESIAN_POINT('Ctrl Pts',(16.7188831698401,18.5581767662136,1.47097694036071));
#182191=CARTESIAN_POINT('Ctrl Pts',(16.6990325458087,18.6273935740738,1.47529572553157));
#182192=CARTESIAN_POINT('Ctrl Pts',(16.6791751531992,18.6966339831755,1.47961598330273));
#182193=CARTESIAN_POINT('Ctrl Pts',(16.6628692969198,18.7668420214691,1.48393624107389));
#182194=CARTESIAN_POINT('Ctrl Pts',(16.6501878706664,18.8376154667879,1.48825649884505));
#182195=CARTESIAN_POINT('Ctrl Pts',(16.6374866781147,18.9084992253316,1.49258349051994));
#182196=CARTESIAN_POINT('Ctrl Pts',(16.6284212609924,18.9799496580401,1.49691048219483));
#182197=CARTESIAN_POINT('Ctrl Pts',(16.6230126894231,19.051558554374,1.50123747386971));
#182198=CARTESIAN_POINT('Ctrl Pts',(16.6189685454458,19.1051025785432,1.5044728895608));
#182199=CARTESIAN_POINT('Ctrl Pts',(16.6169678502349,19.1587350720429,1.50770830525189));
#182200=CARTESIAN_POINT('Ctrl Pts',(16.6170003908423,19.2122864004549,1.51094372094299));
#182201=CARTESIAN_POINT('Ctrl Pts',(16.7454193623539,19.9371102172391,0.534177402122746));
#182202=CARTESIAN_POINT('Ctrl Pts',(16.756562724423,19.9676282756865,0.535943849822347));
#182203=CARTESIAN_POINT('Ctrl Pts',(16.7684072898019,19.9978861948824,0.537705174453422));
#182204=CARTESIAN_POINT('Ctrl Pts',(16.8090263026562,20.0950034808735,0.543420741127037));
#182205=CARTESIAN_POINT('Ctrl Pts',(16.8405517695276,20.1606520575966,0.547383534943635));
#182206=CARTESIAN_POINT('Ctrl Pts',(16.9018328518271,20.2730273714616,0.554496494854256));
#182207=CARTESIAN_POINT('Ctrl Pts',(16.9301570205818,20.3204541225289,0.557608838259091));
#182208=CARTESIAN_POINT('Ctrl Pts',(16.9790300138036,20.3954603342754,0.562757572606629));
#182209=CARTESIAN_POINT('Ctrl Pts',(16.9984537533276,20.423742744312,0.564754091846472));
#182210=CARTESIAN_POINT('Ctrl Pts',(17.0248616471255,20.460260144395,0.56741141665792));
#182211=CARTESIAN_POINT('Ctrl Pts',(17.0312342977272,20.4689323409034,0.568048528655164));
#182212=CARTESIAN_POINT('Ctrl Pts',(17.0417745265414,20.4830491155063,0.56909576419284));
#182213=CARTESIAN_POINT('Ctrl Pts',(17.0459029725942,20.4885227706915,0.569504346541613));
#182214=CARTESIAN_POINT('Ctrl Pts',(17.0539417347487,20.4990738703718,0.570296888908976));
#182215=CARTESIAN_POINT('Ctrl Pts',(17.0578486655817,20.5041538086753,0.57068071187744));
#182216=CARTESIAN_POINT('Ctrl Pts',(17.0669165426598,20.5158340681388,0.571568473305868));
#182217=CARTESIAN_POINT('Ctrl Pts',(17.0720937011993,20.5224216141067,0.572073057614116));
#182218=CARTESIAN_POINT('Ctrl Pts',(17.0861068718921,20.5400360809601,0.573432879666399));
#182219=CARTESIAN_POINT('Ctrl Pts',(17.0950142907443,20.551005408837,0.57429099364533));
#182220=CARTESIAN_POINT('Ctrl Pts',(17.1997115698296,20.6773325280239,0.584307127282494));
#182221=CARTESIAN_POINT('Ctrl Pts',(17.3073680119756,20.7822661100089,0.593981625988371));
#182222=CARTESIAN_POINT('Ctrl Pts',(17.4998930276581,20.9337027526133,0.610137964852008));
#182223=CARTESIAN_POINT('Ctrl Pts',(17.5784805043172,20.9873727236999,0.616463116035545));
#182224=CARTESIAN_POINT('Ctrl Pts',(17.6992044460439,21.0584071728718,0.62558485400973));
#182225=CARTESIAN_POINT('Ctrl Pts',(17.7387199493818,21.0799925750724,0.62848263433545));
#182226=CARTESIAN_POINT('Ctrl Pts',(17.8009176767065,21.1114355468572,0.632877777298203));
#182227=CARTESIAN_POINT('Ctrl Pts',(17.8231334431907,21.1221829136802,0.634415899125118));
#182228=CARTESIAN_POINT('Ctrl Pts',(17.8514890955971,21.1352937823555,0.63633456896334));
#182229=CARTESIAN_POINT('Ctrl Pts',(17.8574579143101,21.138019987403,0.636735977221417));
#182230=CARTESIAN_POINT('Ctrl Pts',(17.8665014919926,21.1420998480894,0.637340332364613));
#182231=CARTESIAN_POINT('Ctrl Pts',(17.8695668896895,21.1434739798638,0.63754452063482));
#182232=CARTESIAN_POINT('Ctrl Pts',(17.8758784656048,21.1462852593308,0.637963556785993));
#182233=CARTESIAN_POINT('Ctrl Pts',(17.8791249403604,21.1477215172385,0.638178342160096));
#182234=CARTESIAN_POINT('Ctrl Pts',(17.8864158931906,21.1509251693241,0.638659042109321));
#182235=CARTESIAN_POINT('Ctrl Pts',(17.8904622900809,21.1526880834597,0.638924680508405));
#182236=CARTESIAN_POINT('Ctrl Pts',(17.9007735587099,21.1571421292849,0.639598759682447));
#182237=CARTESIAN_POINT('Ctrl Pts',(17.9070460265367,21.159815696384,0.640006153946092));
#182238=CARTESIAN_POINT('Ctrl Pts',(17.9427413969337,21.1748270650212,0.642310098073665));
#182239=CARTESIAN_POINT('Ctrl Pts',(17.9724290328811,21.1865295053802,0.644170670350717));
#182240=CARTESIAN_POINT('Ctrl Pts',(18.1885440303228,21.2661224211325,0.657394732742192));
#182241=CARTESIAN_POINT('Ctrl Pts',(18.3834475168518,21.3081844708969,0.667705160540902));
#182242=CARTESIAN_POINT('Ctrl Pts',(18.637122459161,21.326520630638,0.681839180760794));
#182243=CARTESIAN_POINT('Ctrl Pts',(18.6930022215356,21.3283406221212,0.6849891144651));
#182244=CARTESIAN_POINT('Ctrl Pts',(18.7835696213148,21.3277037771267,0.690198378493945));
#182245=CARTESIAN_POINT('Ctrl Pts',(18.8182406329936,21.3266075582574,0.692217108574196));
#182246=CARTESIAN_POINT('Ctrl Pts',(18.8637192659375,21.324049938197,0.694903406692536));
#182247=CARTESIAN_POINT('Ctrl Pts',(18.8745658310064,21.3233561181223,0.695546938774921));
#182248=CARTESIAN_POINT('Ctrl Pts',(18.8923112791503,21.3220837172094,0.696604641425374));
#182249=CARTESIAN_POINT('Ctrl Pts',(18.8992136022352,21.3215547578925,0.697017252603233));
#182250=CARTESIAN_POINT('Ctrl Pts',(18.9125618877222,21.3204659312838,0.697817573212983));
#182251=CARTESIAN_POINT('Ctrl Pts',(18.9190081293011,21.3199103474658,0.698205143869197));
#182252=CARTESIAN_POINT('Ctrl Pts',(18.9338756702912,21.3185602637672,0.699101555770323));
#182253=CARTESIAN_POINT('Ctrl Pts',(18.9422949152877,21.3177448288805,0.699611049189496));
#182254=CARTESIAN_POINT('Ctrl Pts',(18.9649012567384,21.3154184859775,0.700984204353337));
#182255=CARTESIAN_POINT('Ctrl Pts',(18.9790781526884,21.3138145990467,0.701850770658813));
#182256=CARTESIAN_POINT('Ctrl Pts',(19.106811711782,21.2980543600734,0.709708819570844));
#182257=CARTESIAN_POINT('Ctrl Pts',(19.2190444174331,21.2748578120664,0.716988278950171));
#182258=CARTESIAN_POINT('Ctrl Pts',(19.4859092918018,21.1967258837588,0.735128312832324));
#182259=CARTESIAN_POINT('Ctrl Pts',(19.6371123258896,21.132682254234,0.746145465618919));
#182260=CARTESIAN_POINT('Ctrl Pts',(19.8079305733085,21.0356743765984,0.758627853763173));
#182261=CARTESIAN_POINT('Ctrl Pts',(19.8360559134626,21.0188264556625,0.760682339621224));
#182262=CARTESIAN_POINT('Ctrl Pts',(19.8699355201268,20.9974468835483,0.763145753105675));
#182263=CARTESIAN_POINT('Ctrl Pts',(19.8760707536261,20.993530889175,0.763591381934539));
#182264=CARTESIAN_POINT('Ctrl Pts',(19.8856545564423,20.9873439502646,0.764286605607547));
#182265=CARTESIAN_POINT('Ctrl Pts',(19.8891168183034,20.985094468668,0.764537580047137));
#182266=CARTESIAN_POINT('Ctrl Pts',(19.8955694360586,20.9808752122556,0.765004944770918));
#182267=CARTESIAN_POINT('Ctrl Pts',(19.8985613494921,20.9789079968479,0.76522149408671));
#182268=CARTESIAN_POINT('Ctrl Pts',(19.9053744241816,20.9744035262513,0.765714268441916));
#182269=CARTESIAN_POINT('Ctrl Pts',(19.9091923301671,20.9718614443066,0.765990165718856));
#182270=CARTESIAN_POINT('Ctrl Pts',(19.9208987848998,20.9640118857327,0.766835470681614));
#182271=CARTESIAN_POINT('Ctrl Pts',(19.9287599901286,20.9586635748104,0.76740220439784));
#182272=CARTESIAN_POINT('Ctrl Pts',(19.998928625162,20.9102301392836,0.772455181903175));
#182273=CARTESIAN_POINT('Ctrl Pts',(20.0589248387729,20.8638775671038,0.776736150494002));
#182274=CARTESIAN_POINT('Ctrl Pts',(20.2235252286147,20.7219736403893,0.788766768780923));
#182275=CARTESIAN_POINT('Ctrl Pts',(20.3211982725721,20.6190236933256,0.796291251981862));
#182276=CARTESIAN_POINT('Ctrl Pts',(20.4457161798494,20.4582123097537,0.80754379327122));
#182277=CARTESIAN_POINT('Ctrl Pts',(20.4814031027039,20.4077006159384,0.811013082959222));
#182278=CARTESIAN_POINT('Ctrl Pts',(20.5349762899166,20.3243561805785,0.816699232903889));
#182279=CARTESIAN_POINT('Ctrl Pts',(20.5542933360489,20.2924848601878,0.818864949667193));
#182280=CARTESIAN_POINT('Ctrl Pts',(20.5782785544778,20.2504468188019,0.821718054571487));
#182281=CARTESIAN_POINT('Ctrl Pts',(20.5837221443767,20.2407286327283,0.822377375253046));
#182282=CARTESIAN_POINT('Ctrl Pts',(20.5924483826058,20.2248576007117,0.823453923213482));
#182283=CARTESIAN_POINT('Ctrl Pts',(20.5957778127629,20.2187306184926,0.823869472658562));
#182284=CARTESIAN_POINT('Ctrl Pts',(20.6021210519353,20.2069187394009,0.824670542748269));
#182285=CARTESIAN_POINT('Ctrl Pts',(20.6051393374452,20.2012363246328,0.825055898523084));
#182286=CARTESIAN_POINT('Ctrl Pts',(20.6119890984084,20.1881973926964,0.825940136923312));
#182287=CARTESIAN_POINT('Ctrl Pts',(20.6158033200074,20.1808319750276,0.82643962238248));
#182288=CARTESIAN_POINT('Ctrl Pts',(20.6258176840739,20.1612123217581,0.827770215726289));
#182289=CARTESIAN_POINT('Ctrl Pts',(20.6319419562772,20.1489199981086,0.828603966026123));
#182290=CARTESIAN_POINT('Ctrl Pts',(20.6774831391373,20.0552393110141,0.834959697891674));
#182291=CARTESIAN_POINT('Ctrl Pts',(20.711763278092,19.9714705122986,0.8406585477474));
#182292=CARTESIAN_POINT('Ctrl Pts',(20.7851878759223,19.753127877923,0.855533026036699));
#182293=CARTESIAN_POINT('Ctrl Pts',(20.8165298322493,19.6163873061826,0.864885018278535));
#182294=CARTESIAN_POINT('Ctrl Pts',(20.8410840997466,19.4229394133724,0.877655839379692));
#182295=CARTESIAN_POINT('Ctrl Pts',(20.8458846130369,19.3680539115681,0.881224599450029));
#182296=CARTESIAN_POINT('Ctrl Pts',(20.8499087233967,19.2846638846011,0.886508591014392));
#182297=CARTESIAN_POINT('Ctrl Pts',(20.8507068063223,19.2562611687222,0.888284013697192));
#182298=CARTESIAN_POINT('Ctrl Pts',(20.8509881595326,19.2209124692084,0.890456401206748));
#182299=CARTESIAN_POINT('Ctrl Pts',(20.8510092763564,19.2139751549177,0.890880956092271));
#182300=CARTESIAN_POINT('Ctrl Pts',(20.8509887259096,19.2029952209623,0.891549956632903));
#182301=CARTESIAN_POINT('Ctrl Pts',(20.8509695805187,19.1989526805118,0.891795631578339));
#182302=CARTESIAN_POINT('Ctrl Pts',(20.8509116365182,19.1913289835508,0.892257713649244));
#182303=CARTESIAN_POINT('Ctrl Pts',(20.8508753308638,19.1877479144022,0.892474251670799));
#182304=CARTESIAN_POINT('Ctrl Pts',(20.8507715425597,19.1795601916312,0.89296818434669));
#182305=CARTESIAN_POINT('Ctrl Pts',(20.8506981096344,19.1749536613371,0.893245243014076));
#182306=CARTESIAN_POINT('Ctrl Pts',(20.8504631740722,19.1627215689918,0.893978808342041));
#182307=CARTESIAN_POINT('Ctrl Pts',(20.8502754963577,19.1550964975247,0.894433888654916));
#182308=CARTESIAN_POINT('Ctrl Pts',(20.8486701978515,19.1016253983308,0.897610763825298));
#182309=CARTESIAN_POINT('Ctrl Pts',(20.8458040228594,19.0558313995566,0.900257365127691));
#182310=CARTESIAN_POINT('Ctrl Pts',(20.8378739168719,18.9726179803269,0.904989142841095));
#182311=CARTESIAN_POINT('Ctrl Pts',(20.8332930773317,18.9351735114383,0.907089570446307));
#182312=CARTESIAN_POINT('Ctrl Pts',(20.8083555701369,18.7684312259721,0.916389477500067));
#182313=CARTESIAN_POINT('Ctrl Pts',(20.777035687811,18.641065964461,0.923366564881029));
#182314=CARTESIAN_POINT('Ctrl Pts',(20.705212815092,18.4339465175242,0.935466838489206));
#182315=CARTESIAN_POINT('Ctrl Pts',(20.6710793765109,18.352388911897,0.940438849597747));
#182316=CARTESIAN_POINT('Ctrl Pts',(20.6228630349491,18.2548061462674,0.946782331582785));
#182317=CARTESIAN_POINT('Ctrl Pts',(20.6135042311001,18.2365390965994,0.947987338026081));
#182318=CARTESIAN_POINT('Ctrl Pts',(20.5997291506858,18.2105889996192,0.949725672894016));
#182319=CARTESIAN_POINT('Ctrl Pts',(20.5955277563891,18.202792758427,0.950251396563604));
#182320=CARTESIAN_POINT('Ctrl Pts',(20.588160908399,18.1893256380738,0.951165662242911));
#182321=CARTESIAN_POINT('Ctrl Pts',(20.5850180281311,18.1836424993534,0.951553393935635));
#182322=CARTESIAN_POINT('Ctrl Pts',(20.5789257769324,18.1727448449794,0.952300606915968));
#182323=CARTESIAN_POINT('Ctrl Pts',(20.5759803200329,18.1675282041279,0.952659944677853));
#182324=CARTESIAN_POINT('Ctrl Pts',(20.5682083863953,18.153898934718,0.953603142492548));
#182325=CARTESIAN_POINT('Ctrl Pts',(20.563346210824,18.1455069202548,0.954188289950987));
#182326=CARTESIAN_POINT('Ctrl Pts',(20.5462827913925,18.1165169130269,0.956225130370639));
#182327=CARTESIAN_POINT('Ctrl Pts',(20.5337902901707,18.0960932858948,0.957687396616656));
#182328=CARTESIAN_POINT('Ctrl Pts',(20.4376925009152,17.9448111592422,0.968729204112628));
#182329=CARTESIAN_POINT('Ctrl Pts',(20.34027644589,17.8233178575756,0.97884485449836));
#182330=CARTESIAN_POINT('Ctrl Pts',(20.1778921519579,17.6610350514906,0.994011792193418));
#182331=CARTESIAN_POINT('Ctrl Pts',(20.1225742907394,17.6112881889482,0.998935581684665));
#182332=CARTESIAN_POINT('Ctrl Pts',(20.0289959185024,17.5356527557143,1.00677230860608));
#182333=CARTESIAN_POINT('Ctrl Pts',(19.9923045519036,17.5079224861622,1.00973306822747));
#182334=CARTESIAN_POINT('Ctrl Pts',(19.9410807314654,17.4717689909137,1.01368767338731));
#182335=CARTESIAN_POINT('Ctrl Pts',(19.9273103184001,17.462292215346,1.014733828231));
#182336=CARTESIAN_POINT('Ctrl Pts',(19.903532099743,17.4463397800455,1.01650952332766));
#182337=CARTESIAN_POINT('Ctrl Pts',(19.8935793863024,17.4397838398172,1.0172437096036));
#182338=CARTESIAN_POINT('Ctrl Pts',(19.8793553338677,17.4305856185229,1.01827957692009));
#182339=CARTESIAN_POINT('Ctrl Pts',(19.8751293491425,17.4278740873655,1.01858566960918));
#182340=CARTESIAN_POINT('Ctrl Pts',(19.8678307253824,17.4232276234403,1.01911139911738));
#182341=CARTESIAN_POINT('Ctrl Pts',(19.8647626966823,17.42128552311,1.01933150900175));
#182342=CARTESIAN_POINT('Ctrl Pts',(19.8588028095985,17.4175342839181,1.01975735882644));
#182343=CARTESIAN_POINT('Ctrl Pts',(19.855911578675,17.4157242425584,1.01996316173796));
#182344=CARTESIAN_POINT('Ctrl Pts',(19.8481018998813,17.410861264295,1.02051699468));
#182345=CARTESIAN_POINT('Ctrl Pts',(19.8431752419216,17.4078214742838,1.02086416357736));
#182346=CARTESIAN_POINT('Ctrl Pts',(19.8248594297354,17.3966239311569,1.02214689192026));
#182347=CARTESIAN_POINT('Ctrl Pts',(19.8113918692479,17.3885945546693,1.023074413435));
#182348=CARTESIAN_POINT('Ctrl Pts',(19.6817562469272,17.3132450594279,1.0318659480391));
#182349=CARTESIAN_POINT('Ctrl Pts',(19.5595044184214,17.2569610832956,1.03912864395588));
#182350=CARTESIAN_POINT('Ctrl Pts',(19.2810394942221,17.1595956316299,1.05514838674519));
#182351=CARTESIAN_POINT('Ctrl Pts',(19.1238252819166,17.1240069057325,1.06389558018213));
#182352=CARTESIAN_POINT('Ctrl Pts',(18.9455568359212,17.1045145556216,1.07436835072972));
#182353=CARTESIAN_POINT('Ctrl Pts',(18.9269811360656,17.1027316417664,1.07546547326997));
#182354=CARTESIAN_POINT('Ctrl Pts',(18.8998844264901,17.1004919792369,1.07707529753234));
#182355=CARTESIAN_POINT('Ctrl Pts',(18.8913800590163,17.099840777574,1.07758189383347));
#182356=CARTESIAN_POINT('Ctrl Pts',(18.8764405353975,17.0987875901689,1.07847428247974));
#182357=CARTESIAN_POINT('Ctrl Pts',(18.8700070065114,17.098363575262,1.07885937815791));
#182358=CARTESIAN_POINT('Ctrl Pts',(18.8574944324215,17.097596300476,1.07960994241787));
#182359=CARTESIAN_POINT('Ctrl Pts',(18.8514156400376,17.0972498638034,1.07997530729846));
#182360=CARTESIAN_POINT('Ctrl Pts',(18.8368538355291,17.0964829803371,1.08085232543758));
#182361=CARTESIAN_POINT('Ctrl Pts',(18.8283696716416,17.0960873541176,1.081364752428));
#182362=CARTESIAN_POINT('Ctrl Pts',(18.7975852360219,17.0948374476746,1.08322945554901));
#182363=CARTESIAN_POINT('Ctrl Pts',(18.77527480158,17.0942847709103,1.08459112651012));
#182364=CARTESIAN_POINT('Ctrl Pts',(18.5696370501641,17.092442947411,1.09724050598387));
#182365=CARTESIAN_POINT('Ctrl Pts',(18.3869095019468,17.114621993147,1.10930507321904));
#182366=CARTESIAN_POINT('Ctrl Pts',(18.1303765751045,17.1802425924788,1.12678910836463));
#182367=CARTESIAN_POINT('Ctrl Pts',(18.0526131915509,17.2049963454408,1.13214926255902));
#182368=CARTESIAN_POINT('Ctrl Pts',(17.942474308772,17.2472023294859,1.13967023409712));
#182369=CARTESIAN_POINT('Ctrl Pts',(17.9088205167623,17.2611042593566,1.14195787922325));
#182370=CARTESIAN_POINT('Ctrl Pts',(17.8686915012132,17.278906231316,1.14465883465502));
#182371=CARTESIAN_POINT('Ctrl Pts',(17.861859245781,17.2819806538699,1.1451177355558));
#182372=CARTESIAN_POINT('Ctrl Pts',(17.8512529387791,17.2868212178856,1.14582847055771));
#182373=CARTESIAN_POINT('Ctrl Pts',(17.8474676156361,17.2885623048334,1.14608179722232));
#182374=CARTESIAN_POINT('Ctrl Pts',(17.8404514779522,17.2918145581987,1.14655069325017));
#182375=CARTESIAN_POINT('Ctrl Pts',(17.837219370951,17.2933227005223,1.1467664385459));
#182376=CARTESIAN_POINT('Ctrl Pts',(17.8299132224204,17.2967543534277,1.14725355243876));
#182377=CARTESIAN_POINT('Ctrl Pts',(17.8258415114156,17.2986826996313,1.14752461795879));
#182378=CARTESIAN_POINT('Ctrl Pts',(17.8135518570699,17.3045511352816,1.14834164841966));
#182379=CARTESIAN_POINT('Ctrl Pts',(17.8053530477413,17.308531366248,1.14888518660741));
#182380=CARTESIAN_POINT('Ctrl Pts',(17.7424065273014,17.3395935525834,1.15304834380841));
#182381=CARTESIAN_POINT('Ctrl Pts',(17.6888228828542,17.3689831792963,1.15653479048717));
#182382=CARTESIAN_POINT('Ctrl Pts',(17.4971417733759,17.4851788360589,1.16906404592256));
#182383=CARTESIAN_POINT('Ctrl Pts',(17.3679313906238,17.5855341478838,1.17766507248722));
#182384=CARTESIAN_POINT('Ctrl Pts',(17.1948923580372,17.755277429185,1.19111361657844));
#182385=CARTESIAN_POINT('Ctrl Pts',(17.1414403898582,17.8139558127117,1.19560092677501));
#182386=CARTESIAN_POINT('Ctrl Pts',(17.0791845688009,17.8905264389171,1.20135956975125));
#182387=CARTESIAN_POINT('Ctrl Pts',(17.0671668158494,17.9057292862489,1.2024982983823));
#182388=CARTESIAN_POINT('Ctrl Pts',(17.0500840151202,17.9279602786127,1.20415785490096));
#182389=CARTESIAN_POINT('Ctrl Pts',(17.0448505108801,17.9348581697942,1.20467202029336));
#182390=CARTESIAN_POINT('Ctrl Pts',(17.0357829761627,17.9469629165049,1.20557306336989));
#182391=CARTESIAN_POINT('Ctrl Pts',(17.0319301869602,17.9521556257389,1.20595920014339));
#182392=CARTESIAN_POINT('Ctrl Pts',(17.0245195163643,17.9622397907126,1.20670835117519));
#182393=CARTESIAN_POINT('Ctrl Pts',(17.0209586865201,17.9671290093577,1.2070712455981));
#182394=CARTESIAN_POINT('Ctrl Pts',(17.0125345137373,17.9788006522251,1.20793681914304));
#182395=CARTESIAN_POINT('Ctrl Pts',(17.0076902571042,17.9855966698619,1.20844022807978));
#182396=CARTESIAN_POINT('Ctrl Pts',(16.9905656820661,18.0099238470477,1.21024028263255));
#182397=CARTESIAN_POINT('Ctrl Pts',(16.9785115262743,18.0276119351793,1.21154550356417));
#182398=CARTESIAN_POINT('Ctrl Pts',(16.8609883967056,18.2058115432035,1.22466377459197));
#182399=CARTESIAN_POINT('Ctrl Pts',(16.7775784210625,18.379759765152,1.23734170243807));
#182400=CARTESIAN_POINT('Ctrl Pts',(16.6954799621187,18.6348874106491,1.25502391933077));
#182401=CARTESIAN_POINT('Ctrl Pts',(16.6761041769799,18.708470376627,1.26000955659167));
#182402=CARTESIAN_POINT('Ctrl Pts',(16.6536719490474,18.8171191060143,1.26707452535752));
#182403=CARTESIAN_POINT('Ctrl Pts',(16.6474610385367,18.8514691274986,1.26926548143157));
#182404=CARTESIAN_POINT('Ctrl Pts',(16.6409663501366,18.8932676544488,1.27186750771622));
#182405=CARTESIAN_POINT('Ctrl Pts',(16.6398690473808,18.9005821205761,1.27232048023146));
#182406=CARTESIAN_POINT('Ctrl Pts',(16.6382167990534,18.9120034350701,1.2730239363616));
#182407=CARTESIAN_POINT('Ctrl Pts',(16.6376355523324,18.9161063336645,1.27327586689129));
#182408=CARTESIAN_POINT('Ctrl Pts',(16.6365763775096,18.9237442393853,1.27374338568317));
#182409=CARTESIAN_POINT('Ctrl Pts',(16.6360953416481,18.9272787126141,1.27395914218768));
#182410=CARTESIAN_POINT('Ctrl Pts',(16.6350235911771,18.9353053093827,1.27444778944548));
#182411=CARTESIAN_POINT('Ctrl Pts',(16.6344383637346,18.9397981127852,1.27472036792849));
#182412=CARTESIAN_POINT('Ctrl Pts',(16.6327408137149,18.9531651309163,1.27552865258896));
#182413=CARTESIAN_POINT('Ctrl Pts',(16.6316702819437,18.9620446814931,1.27606206003475));
#182414=CARTESIAN_POINT('Ctrl Pts',(16.6239226730706,19.029924671547,1.28011460872583));
#182415=CARTESIAN_POINT('Ctrl Pts',(16.6196735815236,19.0891814573785,1.28350785079841));
#182416=CARTESIAN_POINT('Ctrl Pts',(16.6173229666297,19.1688226796919,1.28796711911347));
#182417=CARTESIAN_POINT('Ctrl Pts',(16.6170159594102,19.1891094974751,1.28909419861729));
#182418=CARTESIAN_POINT('Ctrl Pts',(16.6168948152935,19.3491947907339,1.29793912363836));
#182419=CARTESIAN_POINT('Ctrl Pts',(16.6306361030147,19.4886587757916,1.30537418782863));
#182420=CARTESIAN_POINT('Ctrl Pts',(16.6757502469593,19.7144696845794,1.31812043168447));
#182421=CARTESIAN_POINT('Ctrl Pts',(16.6991412224403,19.801948935857,1.32323611985921));
#182422=CARTESIAN_POINT('Ctrl Pts',(16.7324404233321,19.9006641777299,1.32934387929102));
#182423=CARTESIAN_POINT('Ctrl Pts',(16.7369541495324,19.9136274082935,1.33015265068163));
#182424=CARTESIAN_POINT('Ctrl Pts',(16.7428594777534,19.9300705448463,1.33118740163996));
#182425=CARTESIAN_POINT('Ctrl Pts',(16.7441347553409,19.9335920948211,1.33140952983418));
#182426=CARTESIAN_POINT('Ctrl Pts',(16.7454193623274,19.9371102171666,1.33163196712539));
#182427=CARTESIAN_POINT('Origin',(18.734,19.211,0.));
#182428=CARTESIAN_POINT('',(16.7454193622815,19.9371102170409,2.35747630371139));
#182429=CARTESIAN_POINT('',(16.7452305776443,19.937179123763,2.13351566305583));
#182430=CARTESIAN_POINT('',(16.7454193623258,19.9371102171621,0.));
#182431=CARTESIAN_POINT('Ctrl Pts',(16.7454193622815,19.9371102170409,2.35747630371138));
#182432=CARTESIAN_POINT('Ctrl Pts',(16.7421916428779,19.9282705393179,2.35692304823925));
#182433=CARTESIAN_POINT('Ctrl Pts',(16.7390229031478,19.919409444425,2.35636787685067));
#182434=CARTESIAN_POINT('Ctrl Pts',(16.7330803316954,19.9024354550413,2.35530316719403));
#182435=CARTESIAN_POINT('Ctrl Pts',(16.7302965276,19.8943263487455,2.35479397698));
#182436=CARTESIAN_POINT('Ctrl Pts',(16.7255041835947,19.8800853364624,2.35389871683677));
#182437=CARTESIAN_POINT('Ctrl Pts',(16.7234742638274,19.8739607037764,2.35351335928524));
#182438=CARTESIAN_POINT('Ctrl Pts',(16.7195884540883,19.8620545243586,2.35276354714619));
#182439=CARTESIAN_POINT('Ctrl Pts',(16.7177293752827,19.8562740787429,2.35239920214096));
#182440=CARTESIAN_POINT('Ctrl Pts',(16.7133468271313,19.8424435261815,2.351526675112));
#182441=CARTESIAN_POINT('Ctrl Pts',(16.7108465737502,19.8343862225071,2.3510177359621));
#182442=CARTESIAN_POINT('Ctrl Pts',(16.7020108002507,19.8052989880253,2.34917805477513));
#182443=CARTESIAN_POINT('Ctrl Pts',(16.6959546542506,19.7841862757418,2.34783823684224));
#182444=CARTESIAN_POINT('Ctrl Pts',(16.6414577133137,19.5824062330039,2.33498641159933));
#182445=CARTESIAN_POINT('Ctrl Pts',(16.6168436530152,19.3961933092232,2.32266064775721));
#182446=CARTESIAN_POINT('Ctrl Pts',(16.6170536898772,19.1462094399707,2.3061586393481));
#182447=CARTESIAN_POINT('Ctrl Pts',(16.6199199086378,19.0832283233664,2.30201614374009));
#182448=CARTESIAN_POINT('Ctrl Pts',(16.6300811390682,18.9707861221989,2.2947363950253));
#182449=CARTESIAN_POINT('Ctrl Pts',(16.6363255948254,18.921275584138,2.29157203981558));
#182450=CARTESIAN_POINT('Ctrl Pts',(16.6455655229157,18.8643135233085,2.28801329018632));
#182451=CARTESIAN_POINT('Ctrl Pts',(16.6468596252141,18.8566059559694,2.28753350617277));
#182452=CARTESIAN_POINT('Ctrl Pts',(16.6489941838508,18.8443100738919,2.28677109956862));
#182453=CARTESIAN_POINT('Ctrl Pts',(16.6498071584168,18.8397171491461,2.28648698330481));
#182454=CARTESIAN_POINT('Ctrl Pts',(16.6512728103321,18.8315934301886,2.28598568261531));
#182455=CARTESIAN_POINT('Ctrl Pts',(16.6519192987997,18.8280615633969,2.28576815044178));
#182456=CARTESIAN_POINT('Ctrl Pts',(16.6533073569953,18.8205858242115,2.28530859973261));
#182457=CARTESIAN_POINT('Ctrl Pts',(16.6540511540512,18.8166424184035,2.28506670962336));
#182458=CARTESIAN_POINT('Ctrl Pts',(16.6560859638992,18.8060203347525,2.28441649108939));
#182459=CARTESIAN_POINT('Ctrl Pts',(16.6573979732943,18.7993456592714,2.28400934259613));
#182460=CARTESIAN_POINT('Ctrl Pts',(16.6640292714419,18.7664484385469,2.28200921024176));
#182461=CARTESIAN_POINT('Ctrl Pts',(16.6698134510644,18.7403207569644,2.28044126551913));
#182462=CARTESIAN_POINT('Ctrl Pts',(16.6879077730099,18.6653517902546,2.27598364097259));
#182463=CARTESIAN_POINT('Ctrl Pts',(16.7014678599552,18.6168290260983,2.27314935350431));
#182464=CARTESIAN_POINT('Ctrl Pts',(16.756810292162,18.4429805862964,2.26303183181702));
#182465=CARTESIAN_POINT('Ctrl Pts',(16.8085640147541,18.3211507605477,2.25599588680572));
#182466=CARTESIAN_POINT('Ctrl Pts',(16.9207548827088,18.1134366353935,2.24300919011769));
#182467=CARTESIAN_POINT('Ctrl Pts',(16.9768431354944,18.0257156875147,2.23716707856686));
#182468=CARTESIAN_POINT('Ctrl Pts',(17.0475681402362,17.9312210206559,2.23025033500863));
#182469=CARTESIAN_POINT('Ctrl Pts',(17.056104121899,17.920049938363,2.22942224329744));
#182470=CARTESIAN_POINT('Ctrl Pts',(17.0699092577066,17.9023513257223,2.22809313104478));
#182471=CARTESIAN_POINT('Ctrl Pts',(17.0751071298142,17.8957685399776,2.22759493212877));
#182472=CARTESIAN_POINT('Ctrl Pts',(17.0843685936553,17.8841817101953,2.22671108816971));
#182473=CARTESIAN_POINT('Ctrl Pts',(17.0884162012368,17.8791649836453,2.22632608715451));
#182474=CARTESIAN_POINT('Ctrl Pts',(17.0968603465692,17.8687963167266,2.22552547830482));
#182475=CARTESIAN_POINT('Ctrl Pts',(17.1012603585654,17.8634473168953,2.2251097324128));
#182476=CARTESIAN_POINT('Ctrl Pts',(17.1126754498701,17.8497082210246,2.22403475706673));
#182477=CARTESIAN_POINT('Ctrl Pts',(17.1197293722189,17.8413507976079,2.22337394535432));
#182478=CARTESIAN_POINT('Ctrl Pts',(17.1499117511812,17.8061480471852,2.22056070805275));
#182479=CARTESIAN_POINT('Ctrl Pts',(17.1736464405703,17.779832252762,2.21838327367008));
#182480=CARTESIAN_POINT('Ctrl Pts',(17.2376865467791,17.7123152911793,2.21259355592549));
#182481=CARTESIAN_POINT('Ctrl Pts',(17.2790313710179,17.6721448524831,2.20893871029385));
#182482=CARTESIAN_POINT('Ctrl Pts',(17.4217681706141,17.5443621044183,2.19659997877115));
#182483=CARTESIAN_POINT('Ctrl Pts',(17.5298270654757,17.4646905569085,2.1876735729432));
#182484=CARTESIAN_POINT('Ctrl Pts',(17.7216270922426,17.3495907987171,2.17297277944647));
#182485=CARTESIAN_POINT('Ctrl Pts',(17.801447271982,17.3083459866533,2.1671522524706));
#182486=CARTESIAN_POINT('Ctrl Pts',(17.8924920006888,17.2684124361835,2.16101025159265));
#182487=CARTESIAN_POINT('Ctrl Pts',(17.9013574903227,17.264595978432,2.1604172500096));
#182488=CARTESIAN_POINT('Ctrl Pts',(17.9144966592135,17.259045969636,2.15954620154277));
#182489=CARTESIAN_POINT('Ctrl Pts',(17.918750254094,17.2572655976455,2.15926541695837));
#182490=CARTESIAN_POINT('Ctrl Pts',(17.9263117559006,17.2541296722974,2.15876845137721));
#182491=CARTESIAN_POINT('Ctrl Pts',(17.9296173090924,17.2527685871322,2.15855193835014));
#182492=CARTESIAN_POINT('Ctrl Pts',(17.93671255248,17.2498680674558,2.15808879236009));
#182493=CARTESIAN_POINT('Ctrl Pts',(17.9405032505194,17.2483312454638,2.15784231756675));
#182494=CARTESIAN_POINT('Ctrl Pts',(17.9509339903075,17.2441375816814,2.15716668800416));
#182495=CARTESIAN_POINT('Ctrl Pts',(17.9575831489717,17.2415033574815,2.15673887665619));
#182496=CARTESIAN_POINT('Ctrl Pts',(17.9933579779158,17.2275396283182,2.15445184939543));
#182497=CARTESIAN_POINT('Ctrl Pts',(18.0227201288014,17.2168217658297,2.1526271060226));
#182498=CARTESIAN_POINT('Ctrl Pts',(18.2073709333748,17.1540177398109,2.14141262205081));
#182499=CARTESIAN_POINT('Ctrl Pts',(18.3680442264973,17.119444862239,2.13275773579844));
#182500=CARTESIAN_POINT('Ctrl Pts',(18.647749584182,17.0925146075893,2.11737622763435));
#182501=CARTESIAN_POINT('Ctrl Pts',(18.765102781162,17.0909889587338,2.11083586759811));
#182502=CARTESIAN_POINT('Ctrl Pts',(18.8962303121261,17.1001767822463,2.10313518861532));
#182503=CARTESIAN_POINT('Ctrl Pts',(18.9104790289181,17.1013202925066,2.10229341748671));
#182504=CARTESIAN_POINT('Ctrl Pts',(18.933136455166,17.1033697723491,2.10094649518382));
#182505=CARTESIAN_POINT('Ctrl Pts',(18.9415533576519,17.1041819953193,2.10044428757857));
#182506=CARTESIAN_POINT('Ctrl Pts',(18.9563884336583,17.1057033277943,2.09955578549437));
#182507=CARTESIAN_POINT('Ctrl Pts',(18.9628086881437,17.1063914197102,2.09917015747445));
#182508=CARTESIAN_POINT('Ctrl Pts',(18.9760805754408,17.107875283648,2.0983706609248));
#182509=CARTESIAN_POINT('Ctrl Pts',(18.982931660299,17.1086751905841,2.09795666625769));
#182510=CARTESIAN_POINT('Ctrl Pts',(19.0005060023557,17.1108142150008,2.09689133169374));
#182511=CARTESIAN_POINT('Ctrl Pts',(19.0112230393153,17.1122019724386,2.09623846326779));
#182512=CARTESIAN_POINT('Ctrl Pts',(19.0558971050588,17.1183349900579,2.09350325063088));
#182513=CARTESIAN_POINT('Ctrl Pts',(19.0897453995607,17.1238225794588,2.0913975931615));
#182514=CARTESIAN_POINT('Ctrl Pts',(19.1775689213188,17.140259135785,2.08584398846928));
#182515=CARTESIAN_POINT('Ctrl Pts',(19.2312739437073,17.1524959508476,2.08235767083882));
#182516=CARTESIAN_POINT('Ctrl Pts',(19.3900380553204,17.1952462725111,2.07178960915063));
#182517=CARTESIAN_POINT('Ctrl Pts',(19.4932692555904,17.2318194244407,2.06455946934908));
#182518=CARTESIAN_POINT('Ctrl Pts',(19.634393389881,17.2944896723399,2.05435925219723));
#182519=CARTESIAN_POINT('Ctrl Pts',(19.6749886672248,17.31409183085,2.0513876085094));
#182520=CARTESIAN_POINT('Ctrl Pts',(19.7364761528521,17.3462421536707,2.04685419159514));
#182521=CARTESIAN_POINT('Ctrl Pts',(19.7578290743788,17.3578798332692,2.0452736925429));
#182522=CARTESIAN_POINT('Ctrl Pts',(19.7915116571956,17.3769973235664,2.04277555976828));
#182523=CARTESIAN_POINT('Ctrl Pts',(19.8039733020188,17.3842395141737,2.04185020593773));
#182524=CARTESIAN_POINT('Ctrl Pts',(19.8483316372979,17.4106283925259,2.03855475772147));
#182525=CARTESIAN_POINT('Ctrl Pts',(19.8797984294329,17.4304890421585,2.036214036563));
#182526=CARTESIAN_POINT('Ctrl Pts',(19.9166855144527,17.4551539522948,2.0334813444334));
#182527=CARTESIAN_POINT('Ctrl Pts',(19.9226233604314,17.4591681359994,2.0330418114839));
#182528=CARTESIAN_POINT('Ctrl Pts',(19.9322725397851,17.4657629527011,2.03232829476937));
#182529=CARTESIAN_POINT('Ctrl Pts',(19.9359961402759,17.4683254146268,2.03205313052908));
#182530=CARTESIAN_POINT('Ctrl Pts',(19.9426431282497,17.4729310977855,2.03156230138629));
#182531=CARTESIAN_POINT('Ctrl Pts',(19.9455695757653,17.4749697917366,2.03134633565539));
#182532=CARTESIAN_POINT('Ctrl Pts',(19.9518919175143,17.4793979908006,2.03088004765549));
#182533=CARTESIAN_POINT('Ctrl Pts',(19.9552859274201,17.4817900864337,2.03062990642015));
#182534=CARTESIAN_POINT('Ctrl Pts',(19.9647365856681,17.4884926071104,2.02993380883579));
#182535=CARTESIAN_POINT('Ctrl Pts',(19.9707776691004,17.4928250197387,2.02948933428373));
#182536=CARTESIAN_POINT('Ctrl Pts',(20.0055339930903,17.5180290960197,2.02693416356667));
#182537=CARTESIAN_POINT('Ctrl Pts',(20.0337452836321,17.5395899038462,2.02486821527087));
#182538=CARTESIAN_POINT('Ctrl Pts',(20.1223163602661,17.6108809289267,2.01836096441317));
#182539=CARTESIAN_POINT('Ctrl Pts',(20.180471695445,17.6632516697405,2.01405444907915));
#182540=CARTESIAN_POINT('Ctrl Pts',(20.3685245510814,17.8524794553587,1.99950158846896));
#182541=CARTESIAN_POINT('Ctrl Pts',(20.4829689215705,18.0033781368208,1.98943100879019));
#182542=CARTESIAN_POINT('Ctrl Pts',(20.5866623369713,18.1863993984059,1.97719285653013));
#182543=CARTESIAN_POINT('Ctrl Pts',(20.5971134214388,18.2055287401437,1.9759148084833));
#182544=CARTESIAN_POINT('Ctrl Pts',(20.6111846233546,18.2322571252334,1.97412909782014));
#182545=CARTESIAN_POINT('Ctrl Pts',(20.6150578370876,18.2397219062003,1.97363038583349));
#182546=CARTESIAN_POINT('Ctrl Pts',(20.6216476391332,18.2526095910884,1.97276930173931));
#182547=CARTESIAN_POINT('Ctrl Pts',(20.6243856087345,18.2580214931434,1.97240768572763));
#182548=CARTESIAN_POINT('Ctrl Pts',(20.6299899663207,18.2692183221425,1.97165944714882));
#182549=CARTESIAN_POINT('Ctrl Pts',(20.6328532201495,18.2750047393109,1.97127271973035));
#182550=CARTESIAN_POINT('Ctrl Pts',(20.6394677986218,18.2885275655266,1.97036879242577));
#182551=CARTESIAN_POINT('Ctrl Pts',(20.6431985299606,18.2962738695449,1.96985088210365));
#182552=CARTESIAN_POINT('Ctrl Pts',(20.655041264629,18.321251617166,1.96818041075684));
#182553=CARTESIAN_POINT('Ctrl Pts',(20.6629677837243,18.3385695000105,1.96702147309343));
#182554=CARTESIAN_POINT('Ctrl Pts',(20.7016803305764,18.4262563710278,1.96114803843375));
#182555=CARTESIAN_POINT('Ctrl Pts',(20.7288509626346,18.4981495322422,1.9563123883028));
#182556=CARTESIAN_POINT('Ctrl Pts',(20.7863169013329,18.6794517145641,1.94407896681212));
#182557=CARTESIAN_POINT('Ctrl Pts',(20.8118368066024,18.7901214493379,1.93657050814318));
#182558=CARTESIAN_POINT('Ctrl Pts',(20.838684788936,18.9722663393065,1.92441465085685));
#182559=CARTESIAN_POINT('Ctrl Pts',(20.8454862070558,19.0427177893555,1.91976443922954));
#182560=CARTESIAN_POINT('Ctrl Pts',(20.8507833979373,19.1574721367558,1.91238827195877));
#182561=CARTESIAN_POINT('Ctrl Pts',(20.8514394498415,19.201619973507,1.90959840157073));
#182562=CARTESIAN_POINT('Ctrl Pts',(20.850590709431,19.2533051170209,1.90641237483187));
#182563=CARTESIAN_POINT('Ctrl Pts',(20.8504264467416,19.260850312004,1.90594927201401));
#182564=CARTESIAN_POINT('Ctrl Pts',(20.8500975219409,19.2729782457116,1.90520829232597));
#182565=CARTESIAN_POINT('Ctrl Pts',(20.8499583145524,19.2775615301487,1.90492904820232));
#182566=CARTESIAN_POINT('Ctrl Pts',(20.8496838918709,19.2857227468474,1.90443324652));
#182567=CARTESIAN_POINT('Ctrl Pts',(20.8495544901033,19.2893008258325,1.90421636759464));
#182568=CARTESIAN_POINT('Ctrl Pts',(20.8492590293721,19.296934347474,1.90375473807953));
#182569=CARTESIAN_POINT('Ctrl Pts',(20.8490903856668,19.3009896355848,1.90351013370199));
#182570=CARTESIAN_POINT('Ctrl Pts',(20.8485987210255,19.3120463909267,1.90284489049644));
#182571=CARTESIAN_POINT('Ctrl Pts',(20.8482525878264,19.3190468513378,1.90242552717083));
#182572=CARTESIAN_POINT('Ctrl Pts',(20.8462782661088,19.3553234555422,1.90026125721361));
#182573=CARTESIAN_POINT('Ctrl Pts',(20.8440766601191,19.3845667511332,1.89854659067145));
#182574=CARTESIAN_POINT('Ctrl Pts',(20.8357346925322,19.4712656403498,1.89352746604681));
#182575=CARTESIAN_POINT('Ctrl Pts',(20.8278489853177,19.5285284139365,1.89029647469377));
#182576=CARTESIAN_POINT('Ctrl Pts',(20.788742703519,19.7461643735881,1.87810454699388));
#182577=CARTESIAN_POINT('Ctrl Pts',(20.741348770102,19.903041153496,1.86945634464088));
#182578=CARTESIAN_POINT('Ctrl Pts',(20.6682810631338,20.0716168596661,1.85913538181585));
#182579=CARTESIAN_POINT('Ctrl Pts',(20.6599039307459,20.0902034043091,1.85798332696463));
#182580=CARTESIAN_POINT('Ctrl Pts',(20.6312618117153,20.1513780538946,1.85414006252209));
#182581=CARTESIAN_POINT('Ctrl Pts',(20.6098433056162,20.1934075884302,1.85141553414203));
#182582=CARTESIAN_POINT('Ctrl Pts',(20.5810086876706,20.2456030633377,1.84790785791638));
#182583=CARTESIAN_POINT('Ctrl Pts',(20.5748807369915,20.2564676911074,1.84717076020984));
#182584=CARTESIAN_POINT('Ctrl Pts',(20.56499553434,20.2736373846039,1.84599450959108));
#182585=CARTESIAN_POINT('Ctrl Pts',(20.5613008304095,20.2799782649969,1.84555761732416));
#182586=CARTESIAN_POINT('Ctrl Pts',(20.5543409904014,20.2917812792063,1.84473964862079));
#182587=CARTESIAN_POINT('Ctrl Pts',(20.5510840430924,20.2972481639976,1.84435887347424));
#182588=CARTESIAN_POINT('Ctrl Pts',(20.5437773004826,20.3093879325525,1.84350901728435));
#182589=CARTESIAN_POINT('Ctrl Pts',(20.5397151630692,20.3160532453395,1.84303948746125));
#182590=CARTESIAN_POINT('Ctrl Pts',(20.5277474085598,20.3354482094954,1.84166459699428));
#182591=CARTESIAN_POINT('Ctrl Pts',(20.5197435074365,20.348116374469,1.84075562142775));
#182592=CARTESIAN_POINT('Ctrl Pts',(20.4518211010642,20.4531346031113,1.83312694610929));
#182593=CARTESIAN_POINT('Ctrl Pts',(20.3849269097415,20.5407523968702,1.82614110006005));
#182594=CARTESIAN_POINT('Ctrl Pts',(20.2087744242698,20.737589066304,1.80894051006129));
#182595=CARTESIAN_POINT('Ctrl Pts',(20.093790390985,20.8408471399132,1.79858371413249));
#182596=CARTESIAN_POINT('Ctrl Pts',(19.9303629427929,20.9581756585949,1.78563722283704));
#182597=CARTESIAN_POINT('Ctrl Pts',(19.8911957173415,20.9843600557152,1.78265478097309));
#182598=CARTESIAN_POINT('Ctrl Pts',(19.8446510339292,21.0132770160377,1.77927640763443));
#182599=CARTESIAN_POINT('Ctrl Pts',(19.8380954080138,21.0173004998691,1.77880430422388));
#182600=CARTESIAN_POINT('Ctrl Pts',(19.8275603628862,21.0236875493102,1.77805175554134));
#182601=CARTESIAN_POINT('Ctrl Pts',(19.8235949394439,21.0260739069185,1.77776987540688));
#182602=CARTESIAN_POINT('Ctrl Pts',(19.8165433605853,21.0302860494207,1.77727110927092));
#182603=CARTESIAN_POINT('Ctrl Pts',(19.8134603555851,21.0321170194716,1.77705388761988));
#182604=CARTESIAN_POINT('Ctrl Pts',(19.8068995904272,21.0359908866476,1.77659343174892));
#182605=CARTESIAN_POINT('Ctrl Pts',(19.8034206477541,21.0380316763177,1.77635033394191));
#182606=CARTESIAN_POINT('Ctrl Pts',(19.7939794401185,21.043533796457,1.77569343488257));
#182607=CARTESIAN_POINT('Ctrl Pts',(19.7880060051588,21.0469760000352,1.77528085567321));
#182608=CARTESIAN_POINT('Ctrl Pts',(19.7578040861663,21.0641839354206,1.77320957268517));
#182609=CARTESIAN_POINT('Ctrl Pts',(19.7333210628913,21.077500224425,1.7715780985201));
#182610=CARTESIAN_POINT('Ctrl Pts',(19.6610868310265,21.1149593768655,1.76688117621785));
#182611=CARTESIAN_POINT('Ctrl Pts',(19.6126727537498,21.1377813258652,1.76387848682696));
#182612=CARTESIAN_POINT('Ctrl Pts',(19.4338614638177,21.2139276885613,1.75312847144989));
#182613=CARTESIAN_POINT('Ctrl Pts',(19.2990960428324,21.256041328324,1.74564122025373));
#182614=CARTESIAN_POINT('Ctrl Pts',(19.0716516178646,21.302896039203,1.73279280139117));
#182615=CARTESIAN_POINT('Ctrl Pts',(18.9810702371879,21.3155168090212,1.72762832630728));
#182616=CARTESIAN_POINT('Ctrl Pts',(18.8762502781846,21.3232601501756,1.72146648929322));
#182617=CARTESIAN_POINT('Ctrl Pts',(18.8625275804191,21.3241395437659,1.72065630407728));
#182618=CARTESIAN_POINT('Ctrl Pts',(18.8405123634133,21.3253351112831,1.71935053622582));
#182619=CARTESIAN_POINT('Ctrl Pts',(18.8322247188535,21.3257363306046,1.71885761924));
#182620=CARTESIAN_POINT('Ctrl Pts',(18.8175087545359,21.3263620634427,1.71797987500258));
#182621=CARTESIAN_POINT('Ctrl Pts',(18.8110813339525,21.3266060214707,1.7175956623554));
#182622=CARTESIAN_POINT('Ctrl Pts',(18.7976905510128,21.3270531758071,1.71679340046814));
#182623=CARTESIAN_POINT('Ctrl Pts',(18.7907271070015,21.3272512995053,1.71637519683166));
#182624=CARTESIAN_POINT('Ctrl Pts',(18.7726478169181,21.327676394513,1.71528672090801));
#182625=CARTESIAN_POINT('Ctrl Pts',(18.7615310417624,21.3278501711727,1.71461479001464));
#182626=CARTESIAN_POINT('Ctrl Pts',(18.7133131946029,21.3282240262187,1.71168858940707));
#182627=CARTESIAN_POINT('Ctrl Pts',(18.6762136545317,21.3275363181911,1.70940674227916));
#182628=CARTESIAN_POINT('Ctrl Pts',(18.5777708330888,21.3231213996842,1.70326734249333));
#182629=CARTESIAN_POINT('Ctrl Pts',(18.516542549804,21.3176977726179,1.69936055696257));
#182630=CARTESIAN_POINT('Ctrl Pts',(18.36174033495,21.2971649520164,1.68927415811314));
#182631=CARTESIAN_POINT('Ctrl Pts',(18.2687866912904,21.2784225407487,1.68301718166094));
#182632=CARTESIAN_POINT('Ctrl Pts',(18.0583073335769,21.2210662665182,1.66860237089002));
#182633=CARTESIAN_POINT('Ctrl Pts',(17.9422606745775,21.1782526002636,1.66046638293103));
#182634=CARTESIAN_POINT('Ctrl Pts',(17.8220625072784,21.1215360673019,1.65225851978827));
#182635=CARTESIAN_POINT('Ctrl Pts',(17.8135548442014,21.1174518818586,1.65167887829982));
#182636=CARTESIAN_POINT('Ctrl Pts',(17.8009689142666,21.1113059935614,1.65082364741596));
#182637=CARTESIAN_POINT('Ctrl Pts',(17.7968696879234,21.1092878220127,1.65054545915621));
#182638=CARTESIAN_POINT('Ctrl Pts',(17.7895785896349,21.10566882322,1.65005134398387));
#182639=CARTESIAN_POINT('Ctrl Pts',(17.7863842100186,21.104073180113,1.64983509944681));
#182640=CARTESIAN_POINT('Ctrl Pts',(17.7795884741099,21.1006570911798,1.64937557413273));
#182641=CARTESIAN_POINT('Ctrl Pts',(17.775988293417,21.0988344349209,1.64913243477582));
#182642=CARTESIAN_POINT('Ctrl Pts',(17.7661608853262,21.0938237806574,1.64846950909021));
#182643=CARTESIAN_POINT('Ctrl Pts',(17.7599441495859,21.0906151585597,1.64805099729787));
#182644=CARTESIAN_POINT('Ctrl Pts',(17.746084520927,21.0833746079779,1.6471196134722));
#182645=CARTESIAN_POINT('Ctrl Pts',(17.738450134856,21.0793265608257,1.64660770179372));
#182646=CARTESIAN_POINT('Ctrl Pts',(17.7149891599453,21.0667020056668,1.64503739217747));
#182647=CARTESIAN_POINT('Ctrl Pts',(17.6992466078717,21.0579700829618,1.64398769200332));
#182648=CARTESIAN_POINT('Ctrl Pts',(17.6390698668063,21.0235808963217,1.63998321147129));
#182649=CARTESIAN_POINT('Ctrl Pts',(17.595460012099,20.9965108250675,1.63709810804985));
#182650=CARTESIAN_POINT('Ctrl Pts',(17.4394665069196,20.8916386457181,1.62668254710155));
#182651=CARTESIAN_POINT('Ctrl Pts',(17.3337055116919,20.8045937384282,1.61941161073459));
#182652=CARTESIAN_POINT('Ctrl Pts',(17.1675665894962,20.6384580563916,1.60645461422335));
#182653=CARTESIAN_POINT('Ctrl Pts',(17.1029964524114,20.5642087881035,1.60091752310745));
#182654=CARTESIAN_POINT('Ctrl Pts',(17.0354275830518,20.4746198254017,1.59434067433861));
#182655=CARTESIAN_POINT('Ctrl Pts',(17.0271440165423,20.4634080631506,1.59351950248195));
#182656=CARTESIAN_POINT('Ctrl Pts',(17.0140749827288,20.4453486965718,1.59219940498084));
#182657=CARTESIAN_POINT('Ctrl Pts',(17.0092181867436,20.4385530389244,1.59170324014818));
#182658=CARTESIAN_POINT('Ctrl Pts',(17.000687933655,20.4264668905444,1.59082174746918));
#182659=CARTESIAN_POINT('Ctrl Pts',(16.9969981445197,20.4211880159669,1.59043705228111));
#182660=CARTESIAN_POINT('Ctrl Pts',(16.9893818306756,20.4101849841693,1.58963582355046));
#182661=CARTESIAN_POINT('Ctrl Pts',(16.9854592604967,20.4044581951228,1.58921914573037));
#182662=CARTESIAN_POINT('Ctrl Pts',(16.9753906772944,20.389602292374,1.58813905962648));
#182663=CARTESIAN_POINT('Ctrl Pts',(16.9692876168749,20.3804444455288,1.58747404038014));
#182664=CARTESIAN_POINT('Ctrl Pts',(16.9434955384188,20.3410808854293,1.58461862004461));
#182665=CARTESIAN_POINT('Ctrl Pts',(16.9245094793968,20.3104238670881,1.58240226714949));
#182666=CARTESIAN_POINT('Ctrl Pts',(16.8765249250203,20.22833015227,1.57648309716843));
#182667=CARTESIAN_POINT('Ctrl Pts',(16.8488808830936,20.1761420687189,1.57273531387891));
#182668=CARTESIAN_POINT('Ctrl Pts',(16.7944884861391,20.0621795251588,1.564593524878));
#182669=CARTESIAN_POINT('Ctrl Pts',(16.7684510840594,20.0001866912494,1.56018933018398));
#182670=CARTESIAN_POINT('Ctrl Pts',(16.7454191763733,19.9371097078984,1.5557606494604));
#182671=CARTESIAN_POINT('',(16.6200798910611,19.2101717422182,2.08900081352829));
#182672=CARTESIAN_POINT('Ctrl Pts',(16.7454193623274,19.9371102171666,1.33163196712539));
#182673=CARTESIAN_POINT('Ctrl Pts',(16.7469780041856,19.9413788322432,1.33190185517408));
#182674=CARTESIAN_POINT('Ctrl Pts',(16.7485503803193,19.9456424013342,1.33217219827261));
#182675=CARTESIAN_POINT('Ctrl Pts',(16.7523808360471,19.9559267329139,1.33282619370626));
#182676=CARTESIAN_POINT('Ctrl Pts',(16.7546526297506,19.9619422979385,1.33321030082241));
#182677=CARTESIAN_POINT('Ctrl Pts',(16.759443395003,19.9744551546147,1.33401258917509));
#182678=CARTESIAN_POINT('Ctrl Pts',(16.7619671077401,19.9809505370368,1.33443092601526));
#182679=CARTESIAN_POINT('Ctrl Pts',(16.7686050697039,19.9977881906055,1.33552028771208));
#182680=CARTESIAN_POINT('Ctrl Pts',(16.7727688570567,20.0081105854564,1.33619297680958));
#182681=CARTESIAN_POINT('Ctrl Pts',(16.7912114292745,20.0528119494043,1.33912754783629));
#182682=CARTESIAN_POINT('Ctrl Pts',(16.8063135111907,20.0868420597437,1.34141720810393));
#182683=CARTESIAN_POINT('Ctrl Pts',(16.8488256597736,20.1762036238896,1.34758320436534));
#182684=CARTESIAN_POINT('Ctrl Pts',(16.877770903168,20.2307611200909,1.35150931277073));
#182685=CARTESIAN_POINT('Ctrl Pts',(16.9832811391662,20.4102161226008,1.36495842821662));
#182686=CARTESIAN_POINT('Ctrl Pts',(17.0704045123377,20.5284143929022,1.37476374100119));
#182687=CARTESIAN_POINT('Ctrl Pts',(17.182161885078,20.6510932466381,1.38559625206135));
#182688=CARTESIAN_POINT('Ctrl Pts',(17.1955077083043,20.6653423239262,1.3868650160503));
#182689=CARTESIAN_POINT('Ctrl Pts',(17.2456814512456,20.7174481782719,1.39153841104537));
#182690=CARTESIAN_POINT('Ctrl Pts',(17.2837281587797,20.7541107583554,1.39489464216723));
#182691=CARTESIAN_POINT('Ctrl Pts',(17.3295906043271,20.7951082083525,1.3986891934953));
#182692=CARTESIAN_POINT('Ctrl Pts',(17.3361072826995,20.8008617937687,1.39922271671008));
#182693=CARTESIAN_POINT('Ctrl Pts',(17.34603362632,20.8095175597638,1.40002662392817));
#182694=CARTESIAN_POINT('Ctrl Pts',(17.3494172701489,20.8124492525178,1.40029912943583));
#182695=CARTESIAN_POINT('Ctrl Pts',(17.3555106790092,20.8176950205516,1.4007870939087));
#182696=CARTESIAN_POINT('Ctrl Pts',(17.3582169959057,20.8200129966446,1.40100283890852));
#182697=CARTESIAN_POINT('Ctrl Pts',(17.3641139352505,20.8250380035355,1.40147081003789));
#182698=CARTESIAN_POINT('Ctrl Pts',(17.3673067240393,20.8277424029174,1.40172284349725));
#182699=CARTESIAN_POINT('Ctrl Pts',(17.3763062231989,20.8353195711663,1.40242955688792));
#182700=CARTESIAN_POINT('Ctrl Pts',(17.3821311849721,20.8401707006116,1.40288268092881));
#182701=CARTESIAN_POINT('Ctrl Pts',(17.417289729973,20.8691329421873,1.40559281767779));
#182702=CARTESIAN_POINT('Ctrl Pts',(17.4472435951132,20.8924842096638,1.40779849604528));
#182703=CARTESIAN_POINT('Ctrl Pts',(17.5483186695137,20.9669959259958,1.41496681029301));
#182704=CARTESIAN_POINT('Ctrl Pts',(17.6219897840333,21.0145513909353,1.41976116469807));
#182705=CARTESIAN_POINT('Ctrl Pts',(17.8507182640593,21.1428388654111,1.43402845752519));
#182706=CARTESIAN_POINT('Ctrl Pts',(18.0130018975068,21.2090848392259,1.44342145627763));
#182707=CARTESIAN_POINT('Ctrl Pts',(18.203829514806,21.260668227523,1.45490743269495));
#182708=CARTESIAN_POINT('Ctrl Pts',(18.2261829610864,21.2663205053858,1.45625813426368));
#182709=CARTESIAN_POINT('Ctrl Pts',(18.2579262484205,21.2737976447255,1.4581853655483));
#182710=CARTESIAN_POINT('Ctrl Pts',(18.2672434705479,21.275925828617,1.4587521460584));
#182711=CARTESIAN_POINT('Ctrl Pts',(18.2824027834644,21.2792805864823,1.45967621913986));
#182712=CARTESIAN_POINT('Ctrl Pts',(18.2882362799591,21.2805456832778,1.46003227186507));
#182713=CARTESIAN_POINT('Ctrl Pts',(18.3004560133001,21.2831416859249,1.46077910482126));
#182714=CARTESIAN_POINT('Ctrl Pts',(18.306843198826,21.2844677766205,1.46117003497336));
#182715=CARTESIAN_POINT('Ctrl Pts',(18.322048551967,21.2875514327962,1.46210207166755));
#182716=CARTESIAN_POINT('Ctrl Pts',(18.3308719352508,21.2892823696739,1.46264402259786));
#182717=CARTESIAN_POINT('Ctrl Pts',(18.3606155230247,21.294920812619,1.46447480700334));
#182718=CARTESIAN_POINT('Ctrl Pts',(18.3815830273768,21.2985689560884,1.46577185151558));
#182719=CARTESIAN_POINT('Ctrl Pts',(18.56002645564,21.3268514647283,1.47686840352228));
#182720=CARTESIAN_POINT('Ctrl Pts',(18.719736661254,21.3339396080834,1.48724143341919));
#182721=CARTESIAN_POINT('Ctrl Pts',(19.009993183724,21.3140540498511,1.50645963799945));
#182722=CARTESIAN_POINT('Ctrl Pts',(19.140175957676,21.2928347141087,1.51519755611925));
#182723=CARTESIAN_POINT('Ctrl Pts',(19.2827889005186,21.2556925418244,1.52439146540134));
#182724=CARTESIAN_POINT('Ctrl Pts',(19.2979796641196,21.2515547823996,1.52536557302689));
#182725=CARTESIAN_POINT('Ctrl Pts',(19.3187008095772,21.2456615412594,1.52668584307872));
#182726=CARTESIAN_POINT('Ctrl Pts',(19.3242717952639,21.2440523440716,1.52703996155975));
#182727=CARTESIAN_POINT('Ctrl Pts',(19.3331111342403,21.2414596762579,1.52760041314962));
#182728=CARTESIAN_POINT('Ctrl Pts',(19.3363837941966,21.240491170947,1.52780760386142));
#182729=CARTESIAN_POINT('Ctrl Pts',(19.3431353897698,21.2384753454715,1.52823438350765));
#182730=CARTESIAN_POINT('Ctrl Pts',(19.3466139729846,21.237426983589,1.5284539042033));
#182731=CARTESIAN_POINT('Ctrl Pts',(19.3548923804098,21.2349088048287,1.5289754838968));
#182732=CARTESIAN_POINT('Ctrl Pts',(19.3596897455866,21.2334308496864,1.52927706824309));
#182733=CARTESIAN_POINT('Ctrl Pts',(19.3758337499603,21.2283943206485,1.53028982671829));
#182734=CARTESIAN_POINT('Ctrl Pts',(19.3871558880309,21.2247571373248,1.53099654832436));
#182735=CARTESIAN_POINT('Ctrl Pts',(19.5221745262441,21.1801244815896,1.53938848306166));
#182736=CARTESIAN_POINT('Ctrl Pts',(19.6418803129861,21.1278811940742,1.54647761906019));
#182737=CARTESIAN_POINT('Ctrl Pts',(19.8981324773847,20.9866162340896,1.56237404472561));
#182738=CARTESIAN_POINT('Ctrl Pts',(20.0307366459323,20.8922151917734,1.57115672268068));
#182739=CARTESIAN_POINT('Ctrl Pts',(20.1688783508615,20.7677196144716,1.58195489211107));
#182740=CARTESIAN_POINT('Ctrl Pts',(20.1862330008015,20.7515424643417,1.5833441127189));
#182741=CARTESIAN_POINT('Ctrl Pts',(20.2102717257774,20.7283675424148,1.5853169836262));
#182742=CARTESIAN_POINT('Ctrl Pts',(20.2171856918803,20.7216100310121,1.58589023946448));
#182743=CARTESIAN_POINT('Ctrl Pts',(20.2283073699279,20.710590061733,1.58682198427699));
#182744=CARTESIAN_POINT('Ctrl Pts',(20.2325437551732,20.7063566403256,1.58717919148745));
#182745=CARTESIAN_POINT('Ctrl Pts',(20.241344768238,20.6974868251186,1.58792612316353));
#182746=CARTESIAN_POINT('Ctrl Pts',(20.2459060943181,20.6928472566641,1.58831598729466));
#182747=CARTESIAN_POINT('Ctrl Pts',(20.2566543318127,20.6818133636003,1.58924124210576));
#182748=CARTESIAN_POINT('Ctrl Pts',(20.2628224252603,20.6754009536247,1.58977744488563));
#182749=CARTESIAN_POINT('Ctrl Pts',(20.2832287128909,20.6539169318808,1.59156905774313));
#182750=CARTESIAN_POINT('Ctrl Pts',(20.2972855530825,20.6386754213347,1.59283220887405));
#182751=CARTESIAN_POINT('Ctrl Pts',(20.3711298304456,20.5562094234078,1.59962720789639));
#182752=CARTESIAN_POINT('Ctrl Pts',(20.4268030090818,20.4854398164007,1.60532705925388));
#182753=CARTESIAN_POINT('Ctrl Pts',(20.5546053111571,20.2997760491549,1.61993439702845));
#182754=CARTESIAN_POINT('Ctrl Pts',(20.6205212450552,20.1810880882199,1.62898763181619));
#182755=CARTESIAN_POINT('Ctrl Pts',(20.7047974341816,19.9877506634228,1.64277917976509));
#182756=CARTESIAN_POINT('Ctrl Pts',(20.7312356335687,19.9170003225781,1.64763729017112));
#182757=CARTESIAN_POINT('Ctrl Pts',(20.7566829070162,19.8359263478053,1.65288547243642));
#182758=CARTESIAN_POINT('Ctrl Pts',(20.7594643792006,19.8268515558295,1.65346848951061));
#182759=CARTESIAN_POINT('Ctrl Pts',(20.7634973726325,19.8133706398942,1.65432771734407));
#182760=CARTESIAN_POINT('Ctrl Pts',(20.764795734358,19.8089788119596,1.65460656180705));
#182761=CARTESIAN_POINT('Ctrl Pts',(20.7670812933886,19.801154395927,1.65510139061855));
#182762=CARTESIAN_POINT('Ctrl Pts',(20.7680740637074,19.7977234958364,1.65531769626575));
#182763=CARTESIAN_POINT('Ctrl Pts',(20.77019076326,19.7903384788437,1.65578184593678));
#182764=CARTESIAN_POINT('Ctrl Pts',(20.7713118568443,19.7863836077578,1.65602952418444));
#182765=CARTESIAN_POINT('Ctrl Pts',(20.77437682753,19.7754500697815,1.65671186730624));
#182766=CARTESIAN_POINT('Ctrl Pts',(20.7762964352237,19.7684645762021,1.65714514397713));
#182767=CARTESIAN_POINT('Ctrl Pts',(20.7866510679994,19.730012410175,1.65951615387513));
#182768=CARTESIAN_POINT('Ctrl Pts',(20.7943952489512,19.6983622573656,1.6614163478016));
#182769=CARTESIAN_POINT('Ctrl Pts',(20.8364044400941,19.507710963868,1.6726249309217));
#182770=CARTESIAN_POINT('Ctrl Pts',(20.8529860108762,19.3453575011157,1.681221689799));
#182771=CARTESIAN_POINT('Ctrl Pts',(20.8492485378129,19.0658729950936,1.69652341869061));
#182772=CARTESIAN_POINT('Ctrl Pts',(20.8380194480306,18.9493989181104,1.70304550621825));
#182773=CARTESIAN_POINT('Ctrl Pts',(20.8147014991038,18.8203921794501,1.71072561347407));
#182774=CARTESIAN_POINT('Ctrl Pts',(20.8120175446922,18.8063566176377,1.71156711398024));
#182775=CARTESIAN_POINT('Ctrl Pts',(20.8075197986346,18.7840619190204,1.71291367999649));
#182776=CARTESIAN_POINT('Ctrl Pts',(20.805798232832,18.7757844676587,1.71341580429983));
#182777=CARTESIAN_POINT('Ctrl Pts',(20.8026745529542,18.7612041759646,1.71430420428939));
#182778=CARTESIAN_POINT('Ctrl Pts',(20.8012930921936,18.7548969865231,1.71468981394865));
#182779=CARTESIAN_POINT('Ctrl Pts',(20.7983761102137,18.7418647756467,1.71548931686087));
#182780=CARTESIAN_POINT('Ctrl Pts',(20.7968365313959,18.7351407496575,1.71590333646829));
#182781=CARTESIAN_POINT('Ctrl Pts',(20.7928002593891,18.7179002940254,1.71696882869623));
#182782=CARTESIAN_POINT('Ctrl Pts',(20.7902558612143,18.7073953390516,1.71762183079105));
#182783=CARTESIAN_POINT('Ctrl Pts',(20.779300133204,18.6636305401481,1.72035839656207));
#182784=CARTESIAN_POINT('Ctrl Pts',(20.7701617750408,18.6305596757707,1.72246530292395));
#182785=CARTESIAN_POINT('Ctrl Pts',(20.7442598257753,18.5449809024626,1.72802300247571));
#182786=CARTESIAN_POINT('Ctrl Pts',(20.7262430089568,18.4928823372306,1.73151223757575));
#182787=CARTESIAN_POINT('Ctrl Pts',(20.6664533522414,18.3396326436658,1.74208588985661));
#182788=CARTESIAN_POINT('Ctrl Pts',(20.6188535678228,18.240958459499,1.7493186861522));
#182789=CARTESIAN_POINT('Ctrl Pts',(20.5394824059182,18.1045327043741,1.75974481558208));
#182790=CARTESIAN_POINT('Ctrl Pts',(20.5136858765388,18.0635005392597,1.76293908883565));
#182791=CARTESIAN_POINT('Ctrl Pts',(20.4766030372342,18.0087790893354,1.76725143628182));
#182792=CARTESIAN_POINT('Ctrl Pts',(20.4665200398357,17.994293462095,1.76839814769748));
#182793=CARTESIAN_POINT('Ctrl Pts',(20.4252329219593,17.9365328701719,1.77298682028713));
#182794=CARTESIAN_POINT('Ctrl Pts',(20.3925763983772,17.8943145292206,1.77637830339518));
#182795=CARTESIAN_POINT('Ctrl Pts',(20.3527644106781,17.8466808199386,1.78020788810544));
#182796=CARTESIAN_POINT('Ctrl Pts',(20.3471307456209,17.8400243452549,1.78074310877312));
#182797=CARTESIAN_POINT('Ctrl Pts',(20.3385386644697,17.8299986339549,1.78154907971394));
#182798=CARTESIAN_POINT('Ctrl Pts',(20.3356104914802,17.8266037658125,1.78182196699794));
#182799=CARTESIAN_POINT('Ctrl Pts',(20.3303352479972,17.8205268872433,1.78231034977937));
#182800=CARTESIAN_POINT('Ctrl Pts',(20.3279921801335,17.8178414908725,1.78252613341665));
#182801=CARTESIAN_POINT('Ctrl Pts',(20.3228863945425,17.8120194799911,1.78299387854626));
#182802=CARTESIAN_POINT('Ctrl Pts',(20.3201211746278,17.8088851365821,1.78324564903745));
#182803=CARTESIAN_POINT('Ctrl Pts',(20.3123283672193,17.8001046388885,1.78395089557332));
#182804=CARTESIAN_POINT('Ctrl Pts',(20.3072797334942,17.7944771308379,1.78440282600401));
#182805=CARTESIAN_POINT('Ctrl Pts',(20.276929880101,17.7610098010537,1.787090943966));
#182806=CARTESIAN_POINT('Ctrl Pts',(20.2509187004627,17.7338194959622,1.78927676090886));
#182807=CARTESIAN_POINT('Ctrl Pts',(20.1629633807314,17.6466520905559,1.7963483171119));
#182808=CARTESIAN_POINT('Ctrl Pts',(20.0980772765486,17.5897608879431,1.80107091205644));
#182809=CARTESIAN_POINT('Ctrl Pts',(19.8902343793694,17.4288646978125,1.81537503209623));
#182810=CARTESIAN_POINT('Ctrl Pts',(19.7376080142937,17.3386622944883,1.82486499111222));
#182811=CARTESIAN_POINT('Ctrl Pts',(19.5545392181901,17.2593521993591,1.83645920381707));
#182812=CARTESIAN_POINT('Ctrl Pts',(19.5333738500598,17.2505880193407,1.83780131860654));
#182813=CARTESIAN_POINT('Ctrl Pts',(19.5032057589267,17.2386657565649,1.83971837261292));
#182814=CARTESIAN_POINT('Ctrl Pts',(19.494317047693,17.2352222164772,1.84028370317441));
#182815=CARTESIAN_POINT('Ctrl Pts',(19.4798294268298,17.2297218670089,1.84120604387949));
#182816=CARTESIAN_POINT('Ctrl Pts',(19.474244484625,17.227628457385,1.84156182335105));
#182817=CARTESIAN_POINT('Ctrl Pts',(19.4625295139323,17.2232936967814,1.84230859841604));
#182818=CARTESIAN_POINT('Ctrl Pts',(19.4563978257604,17.2210570409227,1.84269974619969));
#182819=CARTESIAN_POINT('Ctrl Pts',(19.4417752064424,17.215799639779,1.84363325416427));
#182820=CARTESIAN_POINT('Ctrl Pts',(19.4332751880835,17.2128047073207,1.84417646599856));
#182821=CARTESIAN_POINT('Ctrl Pts',(19.4045223054752,17.202879724896,1.84601604998599));
#182822=CARTESIAN_POINT('Ctrl Pts',(19.3841840465882,17.1962027759157,1.84732074175406));
#182823=CARTESIAN_POINT('Ctrl Pts',(19.2725582188344,17.1614227213189,1.85450262999146));
#182824=CARTESIAN_POINT('Ctrl Pts',(19.1795617834052,17.1392175769133,1.86057000651584));
#182825=CARTESIAN_POINT('Ctrl Pts',(18.9174228140019,17.0950938246616,1.87784603494144));
#182826=CARTESIAN_POINT('Ctrl Pts',(18.7466635818049,17.0871969393988,1.88933835478954));
#182827=CARTESIAN_POINT('Ctrl Pts',(18.5401924715562,17.1025703036216,1.90255195357782));
#182828=CARTESIAN_POINT('Ctrl Pts',(18.5036512627533,17.1062489512997,1.90486145989074));
#182829=CARTESIAN_POINT('Ctrl Pts',(18.4601412063994,17.1117760230161,1.90756232652012));
#182830=CARTESIAN_POINT('Ctrl Pts',(18.4530650517299,17.1127112919025,1.90800001532627));
#182831=CARTESIAN_POINT('Ctrl Pts',(18.441524560895,17.1142960469123,1.90871114363025));
#182832=CARTESIAN_POINT('Ctrl Pts',(18.4370573982327,17.1149240372782,1.90898575073626));
#182833=CARTESIAN_POINT('Ctrl Pts',(18.4290626635575,17.1160740021586,1.90947598072661));
#182834=CARTESIAN_POINT('Ctrl Pts',(18.4255343847336,17.1165906129906,1.90969190133198));
#182835=CARTESIAN_POINT('Ctrl Pts',(18.4178938842344,17.1177290620179,1.91015854020462));
#182836=CARTESIAN_POINT('Ctrl Pts',(18.4137821975803,17.1183541016403,1.91040907503212));
#182837=CARTESIAN_POINT('Ctrl Pts',(18.4022961757809,17.1201347990691,1.91110737980264));
#182838=CARTESIAN_POINT('Ctrl Pts',(18.3949259874871,17.1213173606338,1.91155365266393));
#182839=CARTESIAN_POINT('Ctrl Pts',(18.3520505285585,17.1284296236444,1.91414009184981));
#182840=CARTESIAN_POINT('Ctrl Pts',(18.3166925806269,17.1352255332595,1.91623421947737));
#182841=CARTESIAN_POINT('Ctrl Pts',(18.2033482143863,17.1600242560738,1.92287118862285));
#182842=CARTESIAN_POINT('Ctrl Pts',(18.1261998397853,17.1815484026885,1.9272729718461));
#182843=CARTESIAN_POINT('Ctrl Pts',(17.8746285671835,17.2673742539128,1.94176382115605));
#182844=CARTESIAN_POINT('Ctrl Pts',(17.707486886663,17.3502299638787,1.95169903594166));
#182845=CARTESIAN_POINT('Ctrl Pts',(17.5349726967251,17.4661474885047,1.96378739445251));
#182846=CARTESIAN_POINT('Ctrl Pts',(17.5168356724065,17.4787506800756,1.96508206419694));
#182847=CARTESIAN_POINT('Ctrl Pts',(17.4920322842555,17.4965681147022,1.96688733410905));
#182848=CARTESIAN_POINT('Ctrl Pts',(17.4851946321198,17.5015422946797,1.96738872126685));
#182849=CARTESIAN_POINT('Ctrl Pts',(17.4734942106061,17.5101616518994,1.9682531929688));
#182850=CARTESIAN_POINT('Ctrl Pts',(17.4686169667912,17.5137870759543,1.96861550756697));
#182851=CARTESIAN_POINT('Ctrl Pts',(17.45876165597,17.5211789642441,1.96935165781247));
#182852=CARTESIAN_POINT('Ctrl Pts',(17.4537845054486,17.5249465449805,1.96972553503268));
#182853=CARTESIAN_POINT('Ctrl Pts',(17.4422554560339,17.5337542330438,1.97059653048465));
#182854=CARTESIAN_POINT('Ctrl Pts',(17.4357163019506,17.5388107864266,1.97109429575));
#182855=CARTESIAN_POINT('Ctrl Pts',(17.4220322084014,17.5495209824846,1.97214392175216));
#182856=CARTESIAN_POINT('Ctrl Pts',(17.4148938318021,17.5551827018701,1.97269609907122));
#182857=CARTESIAN_POINT('Ctrl Pts',(17.3959866774258,17.5703785478384,1.9741711358098));
#182858=CARTESIAN_POINT('Ctrl Pts',(17.3842834573516,17.5799930605662,1.97509721038692));
#182859=CARTESIAN_POINT('Ctrl Pts',(17.3489064523796,17.6096977509895,1.97793713997375));
#182860=CARTESIAN_POINT('Ctrl Pts',(17.3255714093268,17.6301831934223,1.97986683265445));
#182861=CARTESIAN_POINT('Ctrl Pts',(17.1785843790634,17.7650591581541,1.99239369235755));
#182862=CARTESIAN_POINT('Ctrl Pts',(17.068523564442,17.8933376442339,2.00358053853695));
#182863=CARTESIAN_POINT('Ctrl Pts',(16.9197543474234,18.1155517291386,2.02119661537595));
#182864=CARTESIAN_POINT('Ctrl Pts',(16.8705008590982,18.2016091889806,2.02764871574891));
#182865=CARTESIAN_POINT('Ctrl Pts',(16.8232353237548,18.2995388988549,2.03436713610169));
#182866=CARTESIAN_POINT('Ctrl Pts',(16.8190812869895,18.3082988768957,2.03496280913001));
#182867=CARTESIAN_POINT('Ctrl Pts',(16.8130369074776,18.3212746848877,2.0358370156457));
#182868=CARTESIAN_POINT('Ctrl Pts',(16.8111000197744,18.3254685176871,2.03611831500184));
#182869=CARTESIAN_POINT('Ctrl Pts',(16.8076882727686,18.3329197560845,2.03661584871558));
#182870=CARTESIAN_POINT('Ctrl Pts',(16.8062079246754,18.3361745887213,2.03683241795747));
#182871=CARTESIAN_POINT('Ctrl Pts',(16.8030539896857,18.3431560089453,2.03729530481816));
#182872=CARTESIAN_POINT('Ctrl Pts',(16.8013829450984,18.3468836841543,2.03754146625164));
#182873=CARTESIAN_POINT('Ctrl Pts',(16.7968258179881,18.3571288185767,2.03821535470679));
#182874=CARTESIAN_POINT('Ctrl Pts',(16.7939618142309,18.3636561223642,2.03864174979378));
#182875=CARTESIAN_POINT('Ctrl Pts',(16.778851067992,18.3985730221803,2.04090763423713));
#182876=CARTESIAN_POINT('Ctrl Pts',(16.7671937061721,18.4272154823405,2.04271340093821));
#182877=CARTESIAN_POINT('Ctrl Pts',(16.7338151901355,18.5146675025509,2.04809760755346));
#182878=CARTESIAN_POINT('Ctrl Pts',(16.714073416347,18.5741986452579,2.05158934566686));
#182879=CARTESIAN_POINT('Ctrl Pts',(16.6439835858626,18.8218627412806,2.06573526308096));
#182880=CARTESIAN_POINT('Ctrl Pts',(16.6170670028706,19.0155969299278,2.07601658232645));
#182881=CARTESIAN_POINT('Ctrl Pts',(16.6170001249202,19.210272736479,2.08722594468162));
#182882=CARTESIAN_POINT('Ctrl Pts',(16.7452305776443,19.937179123763,2.13351566305583));
#182883=CARTESIAN_POINT('Ctrl Pts',(16.6631152304279,19.7049844831246,2.11869586837805));
#182884=CARTESIAN_POINT('Ctrl Pts',(16.6210475619504,19.4574404220335,2.10387607370028));
#182885=CARTESIAN_POINT('Ctrl Pts',(16.6201761352154,19.2101685860996,2.0890562790225));
#182886=CARTESIAN_POINT('Origin',(18.734,19.211,0.));
#182887=CARTESIAN_POINT('',(16.7454192904825,19.9371100204066,3.1547244898053));
#182888=CARTESIAN_POINT('',(16.7454193815904,19.9371102699217,2.93545674419276));
#182889=CARTESIAN_POINT('',(16.7454193623258,19.9371102171621,0.));
#182890=CARTESIAN_POINT('',(16.6170000449367,19.2105638097622,3.11292712502269));
#182891=CARTESIAN_POINT('Ctrl Pts',(16.7454192904822,19.9371100204058,3.15472448980525));
#182892=CARTESIAN_POINT('Ctrl Pts',(16.6825886116752,19.7650370943612,3.14472559793947));
#182893=CARTESIAN_POINT('Ctrl Pts',(16.6422996596358,19.5853832163324,3.13494345425051));
#182894=CARTESIAN_POINT('Ctrl Pts',(16.6232302297006,19.3755532516873,3.1227499899056));
#182895=CARTESIAN_POINT('Ctrl Pts',(16.6212927655662,19.3484584959526,3.1211629789051));
#182896=CARTESIAN_POINT('Ctrl Pts',(16.6193445971681,19.3111296954677,3.11895643238462));
#182897=CARTESIAN_POINT('Ctrl Pts',(16.6188859031343,19.3009209671181,3.11835092389697));
#182898=CARTESIAN_POINT('Ctrl Pts',(16.6182717244409,19.2846205874733,3.11738067097006));
#182899=CARTESIAN_POINT('Ctrl Pts',(16.6180685939078,19.2785308108873,3.11701742332083));
#182900=CARTESIAN_POINT('Ctrl Pts',(16.6177137006786,19.2663076837147,3.11628676152292));
#182901=CARTESIAN_POINT('Ctrl Pts',(16.6175623043752,19.2601743823862,3.11591933948709));
#182902=CARTESIAN_POINT('Ctrl Pts',(16.617282543914,19.2464168826775,3.11509337012116));
#182903=CARTESIAN_POINT('Ctrl Pts',(16.6171687079842,19.238792503409,3.11463437185928));
#182904=CARTESIAN_POINT('Ctrl Pts',(16.6170306368109,19.224299891525,3.11375947315431));
#182905=CARTESIAN_POINT('Ctrl Pts',(16.6169986298382,19.217431829944,3.11334382362381));
#182906=CARTESIAN_POINT('Ctrl Pts',(16.6170000449367,19.2105638097622,3.11292712502269));
#182907=CARTESIAN_POINT('Ctrl Pts',(16.6170000447698,19.2105646206611,3.11292717422179));
#182908=CARTESIAN_POINT('Ctrl Pts',(16.6170022358522,19.1999106439826,3.11228077304953));
#182909=CARTESIAN_POINT('Ctrl Pts',(16.6170848523641,19.189256952315,3.11163185797907));
#182910=CARTESIAN_POINT('Ctrl Pts',(16.617578463977,19.1570039612813,3.10965950800197));
#182911=CARTESIAN_POINT('Ctrl Pts',(16.6182396504169,19.135410453098,3.10832836959221));
#182912=CARTESIAN_POINT('Ctrl Pts',(16.6268211686643,18.9486429508904,3.0967206675243));
#182913=CARTESIAN_POINT('Ctrl Pts',(16.653738701196,18.7849385490117,3.08584003822765));
#182914=CARTESIAN_POINT('Ctrl Pts',(16.7229664099705,18.5441422443587,3.06928820566192));
#182915=CARTESIAN_POINT('Ctrl Pts',(16.7514475268371,18.4637096097316,3.06367451624404));
#182916=CARTESIAN_POINT('Ctrl Pts',(16.7992807838426,18.3507981705593,3.05584845144454));
#182917=CARTESIAN_POINT('Ctrl Pts',(16.8147682333084,18.3167766190301,3.05349838712842));
#182918=CARTESIAN_POINT('Ctrl Pts',(16.8344565103413,18.2763982294107,3.05073418849401));
#182919=CARTESIAN_POINT('Ctrl Pts',(16.8377998991885,18.269633376248,3.05027194497506));
#182920=CARTESIAN_POINT('Ctrl Pts',(16.8430499687137,18.2591521007839,3.04955726673714));
#182921=CARTESIAN_POINT('Ctrl Pts',(16.8449315586639,18.2554232795284,3.04930331101138));
#182922=CARTESIAN_POINT('Ctrl Pts',(16.8484392813086,18.2485227380709,3.04883392980308));
#182923=CARTESIAN_POINT('Ctrl Pts',(16.8500623741091,18.2453495841412,3.04861832422634));
#182924=CARTESIAN_POINT('Ctrl Pts',(16.8537470662463,18.2381906451431,3.04813241718085));
#182925=CARTESIAN_POINT('Ctrl Pts',(16.8558133232472,18.2342073178473,3.04786241320548));
#182926=CARTESIAN_POINT('Ctrl Pts',(16.8619409706261,18.2224857795106,3.04706886341686));
#182927=CARTESIAN_POINT('Ctrl Pts',(16.8660376864509,18.21476600405,3.04654749332886));
#182928=CARTESIAN_POINT('Ctrl Pts',(16.8957248933654,18.1596509685486,3.04283265561891));
#182929=CARTESIAN_POINT('Ctrl Pts',(16.9230704567465,18.113217968088,3.03974256746979));
#182930=CARTESIAN_POINT('Ctrl Pts',(17.0431963457532,17.9259724041349,3.02723686434036));
#182931=CARTESIAN_POINT('Ctrl Pts',(17.1508610506887,17.7954464955516,3.01836477575473));
#182932=CARTESIAN_POINT('Ctrl Pts',(17.3157914500564,17.6381394297858,3.0057328892593));
#182933=CARTESIAN_POINT('Ctrl Pts',(17.3604032780398,17.5990331474007,3.00239916825214));
#182934=CARTESIAN_POINT('Ctrl Pts',(17.4347742939646,17.5391716443286,2.99691537414576));
#182935=CARTESIAN_POINT('Ctrl Pts',(17.4635284852218,17.5172174322036,2.99481187324192));
#182936=CARTESIAN_POINT('Ctrl Pts',(17.49944302071,17.4912253906929,2.99219808287639));
#182937=CARTESIAN_POINT('Ctrl Pts',(17.5060838158974,17.4864776070072,2.99171533769635));
#182938=CARTESIAN_POINT('Ctrl Pts',(17.5189478807948,17.4773925222532,2.99078117999397));
#182939=CARTESIAN_POINT('Ctrl Pts',(17.5251673367488,17.473050021074,2.99032997530338));
#182940=CARTESIAN_POINT('Ctrl Pts',(17.5314512392659,17.4687125723419,2.98987449873408));
#182941=CARTESIAN_POINT('Ctrl Pts',(17.5314925441408,17.468684063919,2.98987150484728));
#182942=CARTESIAN_POINT('Ctrl Pts',(17.5315768734892,17.4686258646419,2.98986539246833));
#182943=CARTESIAN_POINT('Ctrl Pts',(17.5316198981255,17.4685961738595,2.98986227396587));
#182944=CARTESIAN_POINT('Ctrl Pts',(17.5317077841706,17.4685355295655,2.98985590386711));
#182945=CARTESIAN_POINT('Ctrl Pts',(17.5317526455997,17.4685045762447,2.989852652271));
#182946=CARTESIAN_POINT('Ctrl Pts',(17.5318443334227,17.4684413190506,2.9898460066985));
#182947=CARTESIAN_POINT('Ctrl Pts',(17.5318911599234,17.4684090153321,2.98984261271621));
#182948=CARTESIAN_POINT('Ctrl Pts',(17.5319869188542,17.4683429607958,2.98983567215982));
#182949=CARTESIAN_POINT('Ctrl Pts',(17.532035851442,17.4683092101251,2.98983212557636));
#182950=CARTESIAN_POINT('Ctrl Pts',(17.5321359783802,17.4682401549831,2.9898248685293));
#182951=CARTESIAN_POINT('Ctrl Pts',(17.5321871727421,17.4682048507912,2.98982115806717));
#182952=CARTESIAN_POINT('Ctrl Pts',(17.5322919949396,17.4681325710724,2.98981356082453));
#182953=CARTESIAN_POINT('Ctrl Pts',(17.5323456230126,17.4680955957052,2.98980967402941));
#182954=CARTESIAN_POINT('Ctrl Pts',(17.5324555034409,17.4680198430686,2.98980171029951));
#182955=CARTESIAN_POINT('Ctrl Pts',(17.5325117560146,17.4679810660143,2.98979763335183));
#182956=CARTESIAN_POINT('Ctrl Pts',(17.5326270977567,17.4679015647688,2.98978927393826));
#182957=CARTESIAN_POINT('Ctrl Pts',(17.5326861871207,17.4678608408577,2.98978499146153));
#182958=CARTESIAN_POINT('Ctrl Pts',(17.5328074395509,17.4677772837584,2.98977620381573));
#182959=CARTESIAN_POINT('Ctrl Pts',(17.5328696027798,17.4677344509305,2.98977169863868));
#182960=CARTESIAN_POINT('Ctrl Pts',(17.5329972684181,17.4676464945229,2.9897624463637));
#182961=CARTESIAN_POINT('Ctrl Pts',(17.5330627710907,17.4676013713019,2.98975769925103));
#182962=CARTESIAN_POINT('Ctrl Pts',(17.5331974145518,17.4675086298381,2.9897479414536));
#182963=CARTESIAN_POINT('Ctrl Pts',(17.5332665555702,17.4674610120575,2.98974293075714));
#182964=CARTESIAN_POINT('Ctrl Pts',(17.5334088131685,17.4673630509814,2.98973262135242));
#182965=CARTESIAN_POINT('Ctrl Pts',(17.5334819301287,17.4673127081403,2.98972732262231));
#182966=CARTESIAN_POINT('Ctrl Pts',(17.5336325228447,17.4672090352814,2.98971640939513));
#182967=CARTESIAN_POINT('Ctrl Pts',(17.5337099990025,17.4671557058178,2.98971079487556));
#182968=CARTESIAN_POINT('Ctrl Pts',(17.5338697470543,17.4670457615125,2.98969921842569));
#182969=CARTESIAN_POINT('Ctrl Pts',(17.533952019471,17.4669891472809,2.98969325646527));
#182970=CARTESIAN_POINT('Ctrl Pts',(17.5341218614312,17.4668722914069,2.98968094882359));
#182971=CARTESIAN_POINT('Ctrl Pts',(17.5342094314499,17.4668120505761,2.98967460311699));
#182972=CARTESIAN_POINT('Ctrl Pts',(17.5343904466872,17.4666875473522,2.98966148612111));
#182973=CARTESIAN_POINT('Ctrl Pts',(17.5344838925254,17.4666232858781,2.98965471479764));
#182974=CARTESIAN_POINT('Ctrl Pts',(17.5346773306777,17.4664902838982,2.98964069795859));
#182975=CARTESIAN_POINT('Ctrl Pts',(17.5347773236958,17.4664215445095,2.98963345240471));
#182976=CARTESIAN_POINT('Ctrl Pts',(17.5400137337795,17.4628224798223,2.98925402426785));
#182977=CARTESIAN_POINT('Ctrl Pts',(17.5451656672636,17.4593148758986,2.98888098255558));
#182978=CARTESIAN_POINT('Ctrl Pts',(17.5569193235446,17.4513883410315,2.98803048541268));
#182979=CARTESIAN_POINT('Ctrl Pts',(17.563530552666,17.4469837360625,2.98755249604682));
#182980=CARTESIAN_POINT('Ctrl Pts',(17.5825872750337,17.4344418554582,2.98617575830628));
#182981=CARTESIAN_POINT('Ctrl Pts',(17.5950937277645,17.426398478788,2.98527351997095));
#182982=CARTESIAN_POINT('Ctrl Pts',(17.6829756194647,17.3711783210871,2.97894129442115));
#182983=CARTESIAN_POINT('Ctrl Pts',(17.7611636702856,17.3286658187697,2.97334119730489));
#182984=CARTESIAN_POINT('Ctrl Pts',(17.9728007499609,17.2303088197515,2.95828433474882));
#182985=CARTESIAN_POINT('Ctrl Pts',(18.1097027478052,17.1829937628595,2.9486215907319));
#182986=CARTESIAN_POINT('Ctrl Pts',(18.3017272040593,17.137930883214,2.93572098062541));
#182987=CARTESIAN_POINT('Ctrl Pts',(18.3535535737208,17.127796552358,2.93230559192251));
#182988=CARTESIAN_POINT('Ctrl Pts',(18.4329899716001,17.1153271677221,2.92722072924385));
#182989=CARTESIAN_POINT('Ctrl Pts',(18.4603548788472,17.1115786096582,2.92549593550986));
#182990=CARTESIAN_POINT('Ctrl Pts',(18.4946139090447,17.1075669612551,2.92337655087486));
#182991=CARTESIAN_POINT('Ctrl Pts',(18.5014450166571,17.1068007623458,2.9229559318332));
#182992=CARTESIAN_POINT('Ctrl Pts',(18.5122856716193,17.105638276262,2.9222916937104));
#182993=CARTESIAN_POINT('Ctrl Pts',(18.5162927576658,17.1052201472015,2.92204687476352));
#182994=CARTESIAN_POINT('Ctrl Pts',(18.523869501796,17.1044513918134,2.92158532925242));
#182995=CARTESIAN_POINT('Ctrl Pts',(18.5274388125086,17.1040984026494,2.92136847784437));
#182996=CARTESIAN_POINT('Ctrl Pts',(18.5356236201462,17.1033099602906,2.92087251471041));
#182997=CARTESIAN_POINT('Ctrl Pts',(18.5402396578402,17.1028805958115,2.92059374766919));
#182998=CARTESIAN_POINT('Ctrl Pts',(18.552544682937,17.1017767917782,2.91985306293506));
#182999=CARTESIAN_POINT('Ctrl Pts',(18.5602360932612,17.1011292259914,2.91939261310972));
#183000=CARTESIAN_POINT('Ctrl Pts',(18.615361245259,17.0967915422639,2.91610950222449));
#183001=CARTESIAN_POINT('Ctrl Pts',(18.662907819489,17.0946590053868,2.91336769521128));
#183002=CARTESIAN_POINT('Ctrl Pts',(18.8710151684416,17.0923477195949,2.90160475788779));
#183003=CARTESIAN_POINT('Ctrl Pts',(19.031232575485,17.1088293059051,2.89313068402648));
#183004=CARTESIAN_POINT('Ctrl Pts',(19.27952085583,17.163351341788,2.87913576518118));
#183005=CARTESIAN_POINT('Ctrl Pts',(19.3695414749106,17.1894802447096,2.87388016513978));
#183006=CARTESIAN_POINT('Ctrl Pts',(19.4774371695767,17.2287187781517,2.86719339279597));
#183007=CARTESIAN_POINT('Ctrl Pts',(19.4972331111016,17.2362562602278,2.86595032402239));
#183008=CARTESIAN_POINT('Ctrl Pts',(19.5252501141197,17.2474081905364,2.8641664457785));
#183009=CARTESIAN_POINT('Ctrl Pts',(19.5335668337337,17.2507800093094,2.86363379513879));
#183010=CARTESIAN_POINT('Ctrl Pts',(19.5478883456293,17.2566926365101,2.86271106875666));
#183011=CARTESIAN_POINT('Ctrl Pts',(19.5539033453923,17.2592085119332,2.86232184191933));
#183012=CARTESIAN_POINT('Ctrl Pts',(19.5654056162361,17.2640820845475,2.86157426508889));
#183013=CARTESIAN_POINT('Ctrl Pts',(19.5708947281593,17.2664352977949,2.86121607082922));
#183014=CARTESIAN_POINT('Ctrl Pts',(19.585159085184,17.2726220923853,2.86028146247286));
#183015=CARTESIAN_POINT('Ctrl Pts',(19.5939183341471,17.276492012189,2.85970380963945));
#183016=CARTESIAN_POINT('Ctrl Pts',(19.623783128052,17.2899294746985,2.85772128238144));
#183017=CARTESIAN_POINT('Ctrl Pts',(19.6447571061295,17.2997837890974,2.85630658819478));
#183018=CARTESIAN_POINT('Ctrl Pts',(19.8208603977366,17.3860803973864,2.84423347168089));
#183019=CARTESIAN_POINT('Ctrl Pts',(19.9662183658207,17.480909681432,2.83289423849767));
#183020=CARTESIAN_POINT('Ctrl Pts',(20.1663040368651,17.649564341385,2.81560267873459));
#183021=CARTESIAN_POINT('Ctrl Pts',(20.2305439069275,17.7110218447689,2.80974511321255));
#183022=CARTESIAN_POINT('Ctrl Pts',(20.3166746267585,17.8044812659972,2.80162753133702));
#183023=CARTESIAN_POINT('Ctrl Pts',(20.3418465338895,17.8333266459226,2.79921925369641));
#183024=CARTESIAN_POINT('Ctrl Pts',(20.37106228502,17.8686983221541,2.79639601807684));
#183025=CARTESIAN_POINT('Ctrl Pts',(20.3758689733621,17.8745820273164,2.79593057915607));
#183026=CARTESIAN_POINT('Ctrl Pts',(20.3832759479575,17.8837489366469,2.79521203995973));
#183027=CARTESIAN_POINT('Ctrl Pts',(20.385898284876,17.8870141259032,2.79495739271188));
#183028=CARTESIAN_POINT('Ctrl Pts',(20.3907339269993,17.8930719321444,2.79448737262402));
#183029=CARTESIAN_POINT('Ctrl Pts',(20.3929498519756,17.8958623319795,2.79427181562138));
#183030=CARTESIAN_POINT('Ctrl Pts',(20.3979314831574,17.9021680683938,2.7937868221346));
#183031=CARTESIAN_POINT('Ctrl Pts',(20.400693092122,17.9056865727529,2.79351767824017));
#183032=CARTESIAN_POINT('Ctrl Pts',(20.4087760818118,17.916052403551,2.79272899282741));
#183033=CARTESIAN_POINT('Ctrl Pts',(20.4140666390407,17.9229238004046,2.79221158735288));
#183034=CARTESIAN_POINT('Ctrl Pts',(20.4509313371465,17.9714173740454,2.78859636504929));
#183035=CARTESIAN_POINT('Ctrl Pts',(20.4810002635095,18.0141669515479,2.78559573874627));
#183036=CARTESIAN_POINT('Ctrl Pts',(20.5206592624741,18.075235686476,2.78149688959111));
#183037=CARTESIAN_POINT('Ctrl Pts',(20.5316079174643,18.0926450880233,2.78034875500697));
#183038=CARTESIAN_POINT('Ctrl Pts',(20.5487952701639,18.1208793198539,2.77851473769732));
#183039=CARTESIAN_POINT('Ctrl Pts',(20.5551946814923,18.1316043780944,2.77782443729203));
#183040=CARTESIAN_POINT('Ctrl Pts',(20.5789341107609,18.1722025378972,2.77523300453677));
#183041=CARTESIAN_POINT('Ctrl Pts',(20.5956373334435,18.202442333369,2.77334633899373));
#183042=CARTESIAN_POINT('Ctrl Pts',(20.6620628127469,18.3299780843604,2.76551783587323));
#183043=CARTESIAN_POINT('Ctrl Pts',(20.7049545171909,18.4306390435408,2.75963434543949));
#183044=CARTESIAN_POINT('Ctrl Pts',(20.7574677469185,18.5862665206151,2.75050070207175));
#183045=CARTESIAN_POINT('Ctrl Pts',(20.7730128620427,18.6390388566448,2.74739931386417));
#183046=CARTESIAN_POINT('Ctrl Pts',(20.7948776477617,18.7255663593186,2.74226454337338));
#183047=CARTESIAN_POINT('Ctrl Pts',(20.8024623955705,18.7589760836889,2.74027036343095));
#183048=CARTESIAN_POINT('Ctrl Pts',(20.8113682688386,18.803143676172,2.73761306896901));
#183049=CARTESIAN_POINT('Ctrl Pts',(20.8134224719187,18.8137495978667,2.73697340715607));
#183050=CARTESIAN_POINT('Ctrl Pts',(20.8166549636292,18.8311515177807,2.73592112264613));
#183051=CARTESIAN_POINT('Ctrl Pts',(20.8178813906035,18.8379384566335,2.7355100388059));
#183052=CARTESIAN_POINT('Ctrl Pts',(20.8201918274489,18.8510911830156,2.73471201337094));
#183053=CARTESIAN_POINT('Ctrl Pts',(20.8212799202028,18.8574561827116,2.73432520660659));
#183054=CARTESIAN_POINT('Ctrl Pts',(20.8237259079851,18.8721694142643,2.73342960032452));
#183055=CARTESIAN_POINT('Ctrl Pts',(20.8250629208647,18.8805209627288,2.73292014362793));
#183056=CARTESIAN_POINT('Ctrl Pts',(20.8285258528103,18.9030146598345,2.73154496279444));
#183057=CARTESIAN_POINT('Ctrl Pts',(20.8305585464184,18.9171705196317,2.73067630480479));
#183058=CARTESIAN_POINT('Ctrl Pts',(20.8479987464014,19.0480368635027,2.72261485166742));
#183059=CARTESIAN_POINT('Ctrl Pts',(20.8537869932468,19.1658025193757,2.71511551805553));
#183060=CARTESIAN_POINT('Ctrl Pts',(20.8441655421086,19.4468842640558,2.69673882015871));
#183061=CARTESIAN_POINT('Ctrl Pts',(20.8196468082345,19.6091428873323,2.68572280871913));
#183062=CARTESIAN_POINT('Ctrl Pts',(20.7685576537369,19.7968531555824,2.67337937413454));
#183063=CARTESIAN_POINT('Ctrl Pts',(20.7597660458441,19.8265655353611,2.67143976672973));
#183064=CARTESIAN_POINT('Ctrl Pts',(20.7481515739078,19.8628690874357,2.66909643757592));
#183065=CARTESIAN_POINT('Ctrl Pts',(20.7459439199124,19.8696513009897,2.66865981095885));
#183066=CARTESIAN_POINT('Ctrl Pts',(20.742417659472,19.8803012780622,2.66797614568826));
#183067=CARTESIAN_POINT('Ctrl Pts',(20.7411220831046,19.8841765294935,2.66772778741347));
#183068=CARTESIAN_POINT('Ctrl Pts',(20.7386717732674,19.8914357911763,2.66726335549497));
#183069=CARTESIAN_POINT('Ctrl Pts',(20.7375197000254,19.894820587778,2.66704713523161));
#183070=CARTESIAN_POINT('Ctrl Pts',(20.7348600112227,19.9025703437701,2.66655282442242));
#183071=CARTESIAN_POINT('Ctrl Pts',(20.7333466878332,19.9069332925427,2.66627507533625));
#183072=CARTESIAN_POINT('Ctrl Pts',(20.7286147903333,19.9204326393194,2.66541726054301));
#183073=CARTESIAN_POINT('Ctrl Pts',(20.7253477241292,19.9295520727174,2.66483999282337));
#183074=CARTESIAN_POINT('Ctrl Pts',(20.6861083649967,20.0367583787596,2.65807647922563));
#183075=CARTESIAN_POINT('Ctrl Pts',(20.6429800471054,20.132089065604,2.65228377325281));
#183076=CARTESIAN_POINT('Ctrl Pts',(20.5861536156766,20.2363875671937,2.6457939407797));
#183077=CARTESIAN_POINT('Ctrl Pts',(20.5791989267153,20.2488504730284,2.64501593719248));
#183078=CARTESIAN_POINT('Ctrl Pts',(20.5179708720893,20.356010932262,2.63829728610142));
#183079=CARTESIAN_POINT('Ctrl Pts',(20.4565755615971,20.4464491632975,2.63241910913415));
#183080=CARTESIAN_POINT('Ctrl Pts',(20.3414554341051,20.5906587606872,2.62215688926952));
#183081=CARTESIAN_POINT('Ctrl Pts',(20.2913185062113,20.6470113559695,2.61788302091295));
#183082=CARTESIAN_POINT('Ctrl Pts',(20.2250211086304,20.7139639102609,2.6123816884117));
#183083=CARTESIAN_POINT('Ctrl Pts',(20.2115771960438,20.7271827256754,2.61127338883033));
#183084=CARTESIAN_POINT('Ctrl Pts',(20.191773460551,20.7461413158502,2.60965027835564));
#183085=CARTESIAN_POINT('Ctrl Pts',(20.1855522875329,20.7520250728618,2.60914172239043));
#183086=CARTESIAN_POINT('Ctrl Pts',(20.1745822689646,20.7622747456841,2.6082471957929));
#183087=CARTESIAN_POINT('Ctrl Pts',(20.1698488161687,20.7666570270911,2.60786193390164));
#183088=CARTESIAN_POINT('Ctrl Pts',(20.1606186148432,20.7751244311557,2.60711202438315));
#183089=CARTESIAN_POINT('Ctrl Pts',(20.1561241601204,20.7792119692059,2.60674748500489));
#183090=CARTESIAN_POINT('Ctrl Pts',(20.1453377017581,20.7889373453293,2.60587403444309));
#183091=CARTESIAN_POINT('Ctrl Pts',(20.1390294582118,20.794556943248,2.6053643625018));
#183092=CARTESIAN_POINT('Ctrl Pts',(20.1161438441494,20.814699824562,2.60351932210781));
#183093=CARTESIAN_POINT('Ctrl Pts',(20.0993740074318,20.8290013891903,2.60217480871766));
#183094=CARTESIAN_POINT('Ctrl Pts',(19.9387498973498,20.9617084909908,2.58936234635044));
#183095=CARTESIAN_POINT('Ctrl Pts',(19.7801029760675,21.060876529379,2.57708792910508));
#183096=CARTESIAN_POINT('Ctrl Pts',(19.5380529547054,21.170983708993,2.55953281888367));
#183097=CARTESIAN_POINT('Ctrl Pts',(19.4637182092824,21.1998565383836,2.55429901582396));
#183098=CARTESIAN_POINT('Ctrl Pts',(19.3537815583048,21.2355613872426,2.54693145611749));
#183099=CARTESIAN_POINT('Ctrl Pts',(19.3193557845428,21.2457817944272,2.54467599502686));
#183100=CARTESIAN_POINT('Ctrl Pts',(19.2774826602851,21.2570623714443,2.54200806441007));
#183101=CARTESIAN_POINT('Ctrl Pts',(19.270270550552,21.2589644846257,2.54155122687397));
#183102=CARTESIAN_POINT('Ctrl Pts',(19.2590227187892,21.2618674824414,2.54084308459988));
#183103=CARTESIAN_POINT('Ctrl Pts',(19.254993928983,21.2628946397,2.54059030235616));
#183104=CARTESIAN_POINT('Ctrl Pts',(19.2475040386427,21.264780737758,2.54012199252891));
#183105=CARTESIAN_POINT('Ctrl Pts',(19.2440438268648,21.2656427941227,2.53990629178585));
#183106=CARTESIAN_POINT('Ctrl Pts',(19.2361998145247,21.2675759675739,2.53941877651676));
#183107=CARTESIAN_POINT('Ctrl Pts',(19.231814768706,21.2686418106745,2.53914726804829));
#183108=CARTESIAN_POINT('Ctrl Pts',(19.2204800439872,21.2713585098487,2.53844803035721));
#183109=CARTESIAN_POINT('Ctrl Pts',(19.2135252930803,21.2729882441161,2.53802148695486));
#183110=CARTESIAN_POINT('Ctrl Pts',(19.1706847542736,21.2827987661309,2.53540860718437));
#183111=CARTESIAN_POINT('Ctrl Pts',(19.1345965599149,21.2900782731145,2.53327039006495));
#183112=CARTESIAN_POINT('Ctrl Pts',(18.9307422692366,21.3256928685882,2.52145078262881));
#183113=CARTESIAN_POINT('Ctrl Pts',(18.760216978574,21.3346661905985,2.51249778701761));
#183114=CARTESIAN_POINT('Ctrl Pts',(18.4950797422142,21.3166453258894,2.49788079193117));
#183115=CARTESIAN_POINT('Ctrl Pts',(18.4002755236487,21.3037135529063,2.49252208513441));
#183116=CARTESIAN_POINT('Ctrl Pts',(18.285702472139,21.2801005024953,2.48571044944164));
#183117=CARTESIAN_POINT('Ctrl Pts',(18.2647965717284,21.2754601367662,2.48445395046341));
#183118=CARTESIAN_POINT('Ctrl Pts',(18.2351964026625,21.2684171226172,2.48265413419981));
#183119=CARTESIAN_POINT('Ctrl Pts',(18.2264411174744,21.2662747315379,2.48211917921149));
#183120=CARTESIAN_POINT('Ctrl Pts',(18.2113698566549,21.2624846664033,2.48119372497678));
#183121=CARTESIAN_POINT('Ctrl Pts',(18.2050472819514,21.2608635622447,2.4808040882778));
#183122=CARTESIAN_POINT('Ctrl Pts',(18.1929620932719,21.2577052922725,2.48005660600392));
#183123=CARTESIAN_POINT('Ctrl Pts',(18.18719827188,21.2561729606385,2.47969892040922));
#183124=CARTESIAN_POINT('Ctrl Pts',(18.1722407381353,21.2521286989304,2.47876757638189));
#183125=CARTESIAN_POINT('Ctrl Pts',(18.16305745215,21.2495790238047,2.47819269623891));
#183126=CARTESIAN_POINT('Ctrl Pts',(18.1318712516456,21.2406931399928,2.47622976472061));
#183127=CARTESIAN_POINT('Ctrl Pts',(18.1099546469103,21.2340621851066,2.47483215411796));
#183128=CARTESIAN_POINT('Ctrl Pts',(17.919796046112,21.173144962901,2.46254277184201));
#183129=CARTESIAN_POINT('Ctrl Pts',(17.7588900937194,21.0983467255474,2.45093552725517));
#183130=CARTESIAN_POINT('Ctrl Pts',(17.5362340003908,20.9587014880308,2.43357159237093));
#183131=CARTESIAN_POINT('Ctrl Pts',(17.4661392761633,20.9085379110295,2.42789867378549));
#183132=CARTESIAN_POINT('Ctrl Pts',(17.3701107109149,20.8305395294917,2.42000161146651));
#183133=CARTESIAN_POINT('Ctrl Pts',(17.3415644532976,20.8060629868257,2.41763723257203));
#183134=CARTESIAN_POINT('Ctrl Pts',(17.3080783589006,20.7757663102908,2.41485850290126));
#183135=CARTESIAN_POINT('Ctrl Pts',(17.3025004690122,20.7706651015895,2.41439546462145));
#183136=CARTESIAN_POINT('Ctrl Pts',(17.2938809534938,20.7626970062596,2.41367982591775));
#183137=CARTESIAN_POINT('Ctrl Pts',(17.2908203595503,20.759850862231,2.41342569804632));
#183138=CARTESIAN_POINT('Ctrl Pts',(17.2851655001153,20.754560913545,2.41295615827412));
#183139=CARTESIAN_POINT('Ctrl Pts',(17.2825689998551,20.752119642985,2.41274056526535));
#183140=CARTESIAN_POINT('Ctrl Pts',(17.2767198206098,20.7465922576952,2.41225488784691));
#183141=CARTESIAN_POINT('Ctrl Pts',(17.273470782648,20.7435023684316,2.41198509970045));
#183142=CARTESIAN_POINT('Ctrl Pts',(17.2639302387924,20.7343712533102,2.41119277204724));
#183143=CARTESIAN_POINT('Ctrl Pts',(17.2576661354987,20.7283013559205,2.41067239826115));
#183144=CARTESIAN_POINT('Ctrl Pts',(17.2133343546395,20.6848095244402,2.40698701006873));
#183145=CARTESIAN_POINT('Ctrl Pts',(17.1766531837023,20.6459949249099,2.40392351029271));
#183146=CARTESIAN_POINT('Ctrl Pts',(17.1324646051439,20.5955434004643,2.40015191131375));
#183147=CARTESIAN_POINT('Ctrl Pts',(17.1235532642104,20.5851678832804,2.39938689994671));
#183148=CARTESIAN_POINT('Ctrl Pts',(17.081112484665,20.5347739555129,2.39571810976276));
#183149=CARTESIAN_POINT('Ctrl Pts',(17.0489694635835,20.4936094878229,2.39286152408738));
#183150=CARTESIAN_POINT('Ctrl Pts',(16.954269844877,20.362617898944,2.38406088147274));
#183151=CARTESIAN_POINT('Ctrl Pts',(16.8971323282311,20.269101834365,2.37816902432726));
#183152=CARTESIAN_POINT('Ctrl Pts',(16.8130787893629,20.1040280832914,2.36786971009912));
#183153=CARTESIAN_POINT('Ctrl Pts',(16.7823335528736,20.0346709197077,2.36357207598258));
#183154=CARTESIAN_POINT('Ctrl Pts',(16.7519971962846,19.9549382833464,2.35859153550039));
#183155=CARTESIAN_POINT('Ctrl Pts',(16.7486782177562,19.946035166375,2.35803489614114));
#183156=CARTESIAN_POINT('Ctrl Pts',(16.7454193622815,19.9371102170409,2.35747630371138));
#183157=CARTESIAN_POINT('',(16.6180380291883,19.2128841872923,2.8890562790225));
#183158=CARTESIAN_POINT('Ctrl Pts',(16.6180380291883,19.2128841872923,2.8890562790225));
#183159=CARTESIAN_POINT('Ctrl Pts',(16.6223668818157,18.7070050427869,2.85866010167885));
#183160=CARTESIAN_POINT('Ctrl Pts',(17.0578065161,17.488911989304,2.78587198877473));
#183161=CARTESIAN_POINT('Ctrl Pts',(19.0938031543631,16.7337290395393,2.67069194031012));
#183162=CARTESIAN_POINT('Ctrl Pts',(21.0117474691636,18.1726377106278,2.54351613362868));
#183163=CARTESIAN_POINT('Ctrl Pts',(20.8399998558895,20.5641793786163,2.41634032694726));
#183164=CARTESIAN_POINT('Ctrl Pts',(18.736128084209,21.7142628689015,2.28916452026583));
#183165=CARTESIAN_POINT('Ctrl Pts',(17.1750895426501,20.864363812569,2.19488963230201));
#183166=CARTESIAN_POINT('Ctrl Pts',(16.7978195750248,20.0858831573232,2.14300667989868));
#183167=CARTESIAN_POINT('Ctrl Pts',(16.7452305776443,19.937179123763,2.13351566305583));
#183168=CARTESIAN_POINT('Ctrl Pts',(16.6170008744739,19.2129241938202,2.88845972389577));
#183169=CARTESIAN_POINT('Ctrl Pts',(16.6170483110913,19.2651139869398,2.89187890939447));
#183170=CARTESIAN_POINT('Ctrl Pts',(16.6190256614439,19.3172837811673,2.8953255352823));
#183171=CARTESIAN_POINT('Ctrl Pts',(16.6324061683838,19.4956946961602,2.90714885683369));
#183172=CARTESIAN_POINT('Ctrl Pts',(16.6532119485831,19.6209701165616,2.91552733173334));
#183173=CARTESIAN_POINT('Ctrl Pts',(16.6881017065402,19.7551794554187,2.92412675351169));
#183174=CARTESIAN_POINT('Ctrl Pts',(16.6911984993194,19.7666915967566,2.92486114697043));
#183175=CARTESIAN_POINT('Ctrl Pts',(16.6957386595639,19.7830183180294,2.92589745161739));
#183176=CARTESIAN_POINT('Ctrl Pts',(16.6971021146366,19.7878546210914,2.92620377127852));
#183177=CARTESIAN_POINT('Ctrl Pts',(16.6994812574396,19.7961800500058,2.92672989900691));
#183178=CARTESIAN_POINT('Ctrl Pts',(16.7004887290258,19.7996714842374,2.92695018057992));
#183179=CARTESIAN_POINT('Ctrl Pts',(16.7024593753537,19.8064354093843,2.9273762108653));
#183180=CARTESIAN_POINT('Ctrl Pts',(16.7034214694763,19.809708166049,2.92758202330274));
#183181=CARTESIAN_POINT('Ctrl Pts',(16.7060381584365,19.8185304964909,2.92813598952883));
#183182=CARTESIAN_POINT('Ctrl Pts',(16.7077076345177,19.8240756775356,2.92848328119213));
#183183=CARTESIAN_POINT('Ctrl Pts',(16.713985996204,19.844623501642,2.92976708448758));
#183184=CARTESIAN_POINT('Ctrl Pts',(16.718739047464,19.8595820249649,2.93069553929684));
#183185=CARTESIAN_POINT('Ctrl Pts',(16.7305868663345,19.8954805026194,2.9329119712285));
#183186=CARTESIAN_POINT('Ctrl Pts',(16.7378417059312,19.9163574730357,2.93419125178592));
#183187=CARTESIAN_POINT('Ctrl Pts',(16.7454193815904,19.9371102699218,2.93545674419276));
#183188=CARTESIAN_POINT('Origin',(18.734,19.211,0.));
#183189=CARTESIAN_POINT('',(16.7454192928009,19.9371100267559,3.95421654644109));
#183190=CARTESIAN_POINT('',(16.7454193623262,19.9371102171633,3.73234496441554));
#183191=CARTESIAN_POINT('',(16.7454193623258,19.9371102171621,0.));
#183192=CARTESIAN_POINT('Ctrl Pts',(16.7454192928009,19.9371100267559,3.95421654644109));
#183193=CARTESIAN_POINT('Ctrl Pts',(16.7247484919563,19.8804993834,3.95029629217742));
#183194=CARTESIAN_POINT('Ctrl Pts',(16.7064930186527,19.8230004891677,3.94643456633113));
#183195=CARTESIAN_POINT('Ctrl Pts',(16.6875909795291,19.7532558190289,3.94195338903305));
#183196=CARTESIAN_POINT('Ctrl Pts',(16.6845683668796,19.7417176730903,3.94121861484773));
#183197=CARTESIAN_POINT('Ctrl Pts',(16.6804108714473,19.7252819748228,3.94018187021498));
#183198=CARTESIAN_POINT('Ctrl Pts',(16.6791957316872,19.7204052204843,3.93987548630145));
#183199=CARTESIAN_POINT('Ctrl Pts',(16.6771318962641,19.7119948202375,3.93934928327177));
#183200=CARTESIAN_POINT('Ctrl Pts',(16.676274915089,19.7084632466605,3.93912899029159));
#183201=CARTESIAN_POINT('Ctrl Pts',(16.6746311950773,19.7016126371222,3.93870296551654));
#183202=CARTESIAN_POINT('Ctrl Pts',(16.6738433838447,19.6982939068827,3.93849716986552));
#183203=CARTESIAN_POINT('Ctrl Pts',(16.6717400398632,19.6893370934564,3.93794330716889));
#183204=CARTESIAN_POINT('Ctrl Pts',(16.6704395973557,19.6836954459169,3.93759610167184));
#183205=CARTESIAN_POINT('Ctrl Pts',(16.6657019231336,19.6627500211767,3.93631295334329));
#183206=CARTESIAN_POINT('Ctrl Pts',(16.662411560615,19.6474130918184,3.93538505674119));
#183207=CARTESIAN_POINT('Ctrl Pts',(16.6325545485702,19.5002904636277,3.92658314420798));
#183208=CARTESIAN_POINT('Ctrl Pts',(16.6184239864913,19.36627406199,3.91931201409377));
#183209=CARTESIAN_POINT('Ctrl Pts',(16.6170404626411,19.2255206712854,3.91166808709353));
#183210=CARTESIAN_POINT('Ctrl Pts',(16.6170066729792,19.21923322756,3.91132665166106));
#183211=CARTESIAN_POINT('Ctrl Pts',(16.6168668543953,19.0671072358186,3.90306442079204));
#183212=CARTESIAN_POINT('Ctrl Pts',(16.631802104662,18.9216640300942,3.89510370491612));
#183213=CARTESIAN_POINT('Ctrl Pts',(16.6664676940301,18.7553942943312,3.88524444627758));
#183214=CARTESIAN_POINT('Ctrl Pts',(16.6717720439157,18.7319570133412,3.8838376637426));
#183215=CARTESIAN_POINT('Ctrl Pts',(16.6797804434919,18.6991743721309,3.88184393431146));
#183216=CARTESIAN_POINT('Ctrl Pts',(16.6821518236525,18.6897490852592,3.88126768217143));
#183217=CARTESIAN_POINT('Ctrl Pts',(16.6860916184554,18.6745335581911,3.88033237414389));
#183218=CARTESIAN_POINT('Ctrl Pts',(16.6876199075611,18.6687330007115,3.87997461950769));
#183219=CARTESIAN_POINT('Ctrl Pts',(16.6908553258924,18.6566615851086,3.87922758648507));
#183220=CARTESIAN_POINT('Ctrl Pts',(16.6925667183177,18.6503919439243,3.87883817304001));
#183221=CARTESIAN_POINT('Ctrl Pts',(16.6966783629367,18.6355975501918,3.87791587509186));
#183222=CARTESIAN_POINT('Ctrl Pts',(16.6991032787632,18.6270798322828,3.87738219263228));
#183223=CARTESIAN_POINT('Ctrl Pts',(16.7073169386805,18.598901295646,3.87560761763461));
#183224=CARTESIAN_POINT('Ctrl Pts',(16.7133376069263,18.5793098055459,3.87435918433686));
#183225=CARTESIAN_POINT('Ctrl Pts',(16.7467230035331,18.4760372034541,3.86769848665262));
#183226=CARTESIAN_POINT('Ctrl Pts',(16.7790003195529,18.3940464914149,3.86212556696613));
#183227=CARTESIAN_POINT('Ctrl Pts',(16.8711049339375,18.1970656689088,3.84804779674571));
#183228=CARTESIAN_POINT('Ctrl Pts',(16.9365619977143,18.0850986568205,3.83941386772588));
#183229=CARTESIAN_POINT('Ctrl Pts',(17.0275745884516,17.9577902590976,3.82914895403899));
#183230=CARTESIAN_POINT('Ctrl Pts',(17.0437452682531,17.936064175417,3.8273808935106));
#183231=CARTESIAN_POINT('Ctrl Pts',(17.0955041292582,17.8692399588405,3.82190406589159));
#183232=CARTESIAN_POINT('Ctrl Pts',(17.1325169023024,17.8252720778985,3.81824351413873));
#183233=CARTESIAN_POINT('Ctrl Pts',(17.1772637435692,17.7763083903759,3.8141505490437));
#183234=CARTESIAN_POINT('Ctrl Pts',(17.1832929408898,17.7697937656368,3.81360563789021));
#183235=CARTESIAN_POINT('Ctrl Pts',(17.192451711867,17.7600216143737,3.81278800044979));
#183236=CARTESIAN_POINT('Ctrl Pts',(17.1955509415179,17.7567359608619,3.81251304570616));
#183237=CARTESIAN_POINT('Ctrl Pts',(17.2011160620806,17.7508737892577,3.81202244275113));
#183238=CARTESIAN_POINT('Ctrl Pts',(17.2035779612589,17.7482935693127,3.81180649487585));
#183239=CARTESIAN_POINT('Ctrl Pts',(17.2089220942576,17.7427208566224,3.81134007798083));
#183240=CARTESIAN_POINT('Ctrl Pts',(17.2118066115013,17.7397306330404,3.81108979089212));
#183241=CARTESIAN_POINT('Ctrl Pts',(17.2198846347658,17.7314057682022,3.81039287430154));
#183242=CARTESIAN_POINT('Ctrl Pts',(17.2250975657347,17.7260899429216,3.80994773226656));
#183243=CARTESIAN_POINT('Ctrl Pts',(17.2554564554609,17.6954567773669,3.80738100367323));
#183244=CARTESIAN_POINT('Ctrl Pts',(17.2812128712832,17.670749315593,3.8053046399847));
#183245=CARTESIAN_POINT('Ctrl Pts',(17.3658597101237,17.5935634073009,3.79874964410138));
#183246=CARTESIAN_POINT('Ctrl Pts',(17.4270649057938,17.5437173060126,3.79440809052466));
#183247=CARTESIAN_POINT('Ctrl Pts',(17.5646431049824,17.443914775174,3.78513861471452));
#183248=CARTESIAN_POINT('Ctrl Pts',(17.6417468694929,17.3952443130942,3.78023168271004));
#183249=CARTESIAN_POINT('Ctrl Pts',(17.8150644189032,17.3008858550108,3.76938604393385));
#183250=CARTESIAN_POINT('Ctrl Pts',(17.9120641973599,17.2571842640412,3.7634234586998));
#183251=CARTESIAN_POINT('Ctrl Pts',(18.0251857159193,17.2161390364554,3.75637195120753));
#183252=CARTESIAN_POINT('Ctrl Pts',(18.0384924579377,17.2114607536288,3.75554117881114));
#183253=CARTESIAN_POINT('Ctrl Pts',(18.0597976434987,17.2042088400867,3.75420857474409));
#183254=CARTESIAN_POINT('Ctrl Pts',(18.0677665199581,17.2015491984163,3.75370958840416));
#183255=CARTESIAN_POINT('Ctrl Pts',(18.0818794455598,17.1969321359447,3.75282483126966));
#183256=CARTESIAN_POINT('Ctrl Pts',(18.0880170368992,17.1949552116812,3.75243970890136));
#183257=CARTESIAN_POINT('Ctrl Pts',(18.1007603303273,17.1909147508947,3.75163932766964));
#183258=CARTESIAN_POINT('Ctrl Pts',(18.1073673029933,17.1888555061092,3.75122393312121));
#183259=CARTESIAN_POINT('Ctrl Pts',(18.124416130665,17.1836333479322,3.7501508906198));
#183260=CARTESIAN_POINT('Ctrl Pts',(18.1348724570303,17.1805187230742,3.74949167123378));
#183261=CARTESIAN_POINT('Ctrl Pts',(18.1791654826141,17.1676970858416,3.74669424986871));
#183262=CARTESIAN_POINT('Ctrl Pts',(18.2132158765687,17.1587544484412,3.74453138797352));
#183263=CARTESIAN_POINT('Ctrl Pts',(18.3030456885866,17.1375420061864,3.73878988404235));
#183264=CARTESIAN_POINT('Ctrl Pts',(18.359123449435,17.1266736494679,3.73516955598228));
#183265=CARTESIAN_POINT('Ctrl Pts',(18.5659650864189,17.095203200325,3.72169996848368));
#183266=CARTESIAN_POINT('Ctrl Pts',(18.7183859622587,17.0886001209964,3.71151209603572));
#183267=CARTESIAN_POINT('Ctrl Pts',(18.892616792953,17.0998308026269,3.70010856489985));
#183268=CARTESIAN_POINT('Ctrl Pts',(18.9150333607664,17.1016347781115,3.69864695010285));
#183269=CARTESIAN_POINT('Ctrl Pts',(18.9885486252538,17.1087315212321,3.6938798584984));
#183270=CARTESIAN_POINT('Ctrl Pts',(19.0394879421606,17.1155273052977,3.69061826221014));
#183271=CARTESIAN_POINT('Ctrl Pts',(19.097897583569,17.1254953651646,3.68696361486686));
#183272=CARTESIAN_POINT('Ctrl Pts',(19.1056541397384,17.126863670949,3.68648004763279));
#183273=CARTESIAN_POINT('Ctrl Pts',(19.1180092285927,17.129114356253,3.68571279068866));
#183274=CARTESIAN_POINT('Ctrl Pts',(19.1226126963703,17.1299687425523,3.68542757795243));
#183275=CARTESIAN_POINT('Ctrl Pts',(19.1307437978061,17.1315057662041,3.68492502876699));
#183276=CARTESIAN_POINT('Ctrl Pts',(19.1342725760946,17.1321821207567,3.68470733863894));
#183277=CARTESIAN_POINT('Ctrl Pts',(19.1417294329537,17.133631054568,3.68424820497023));
#183278=CARTESIAN_POINT('Ctrl Pts',(19.1456570398177,17.1344057911757,3.68400688603866));
#183279=CARTESIAN_POINT('Ctrl Pts',(19.1562098319579,17.1365184888115,3.68335982343204));
#183280=CARTESIAN_POINT('Ctrl Pts',(19.1628309110881,17.1378770574379,3.68295524001349));
#183281=CARTESIAN_POINT('Ctrl Pts',(19.1951330106125,17.1446664483656,3.68098774818565));
#183282=CARTESIAN_POINT('Ctrl Pts',(19.2207192523852,17.1505431302219,3.67944890677708));
#183283=CARTESIAN_POINT('Ctrl Pts',(19.2936960197621,17.1687398749753,3.67509903816515));
#183284=CARTESIAN_POINT('Ctrl Pts',(19.3407791790556,17.1822304933156,3.67234024881934));
#183285=CARTESIAN_POINT('Ctrl Pts',(19.4792647697274,17.2271637842869,3.66425653601295));
#183286=CARTESIAN_POINT('Ctrl Pts',(19.5690283484965,17.2632436453111,3.65905330180025));
#183287=CARTESIAN_POINT('Ctrl Pts',(19.782982813211,17.3667607798955,3.64612001393885));
#183288=CARTESIAN_POINT('Ctrl Pts',(19.9034744994948,17.4407160945882,3.63834020669294));
#183289=CARTESIAN_POINT('Ctrl Pts',(20.0270791540754,17.5347424712454,3.62924194329472));
#183290=CARTESIAN_POINT('Ctrl Pts',(20.0383587969921,17.5435045381674,3.62840084155293));
#183291=CARTESIAN_POINT('Ctrl Pts',(20.0561711904685,17.5576325904661,3.627054790234));
#183292=CARTESIAN_POINT('Ctrl Pts',(20.0627620755106,17.562924822304,3.62655277820123));
#183293=CARTESIAN_POINT('Ctrl Pts',(20.0743311130781,17.5723288329612,3.6256645038507));
#183294=CARTESIAN_POINT('Ctrl Pts',(20.0793225079471,17.5764242034842,3.62527890689492));
#183295=CARTESIAN_POINT('Ctrl Pts',(20.0896084815458,17.5849427313107,3.62447935857138));
#183296=CARTESIAN_POINT('Ctrl Pts',(20.094900323121,17.589369060152,3.62406528049336));
#183297=CARTESIAN_POINT('Ctrl Pts',(20.108430224941,17.6007989344874,3.62299948651327));
#183298=CARTESIAN_POINT('Ctrl Pts',(20.1166363606182,17.6078398077196,3.62234623953733));
#183299=CARTESIAN_POINT('Ctrl Pts',(20.1506783955552,17.6375036984667,3.61960735803053));
#183300=CARTESIAN_POINT('Ctrl Pts',(20.1760146505218,17.6606897671486,3.61749833195349));
#183301=CARTESIAN_POINT('Ctrl Pts',(20.240566403812,17.7227151087219,3.61193372246401));
#183302=CARTESIAN_POINT('Ctrl Pts',(20.2788449608135,17.7624878428033,3.60843957879383));
#183303=CARTESIAN_POINT('Ctrl Pts',(20.3882887482446,17.8854814578889,3.5978564865706));
#183304=CARTESIAN_POINT('Ctrl Pts',(20.4545968905746,17.9727699954585,3.59061919264036));
#183305=CARTESIAN_POINT('Ctrl Pts',(20.5427431078368,18.109644338915,3.57986512411882));
#183306=CARTESIAN_POINT('Ctrl Pts',(20.5699267616361,18.1555810368668,3.5763483951389));
#183307=CARTESIAN_POINT('Ctrl Pts',(20.6014103935018,18.2136888882982,3.57204734140284));
#183308=CARTESIAN_POINT('Ctrl Pts',(20.6073733705971,18.2249354710971,3.57122155100634));
#183309=CARTESIAN_POINT('Ctrl Pts',(20.6377306323513,18.2834607935749,3.56696093570361));
#183310=CARTESIAN_POINT('Ctrl Pts',(20.6604400707671,18.3315973715193,3.5635792945492));
#183311=CARTESIAN_POINT('Ctrl Pts',(20.6847307402026,18.3885557957642,3.55975955703126));
#183312=CARTESIAN_POINT('Ctrl Pts',(20.6880986552157,18.3965901882168,3.55922487991935));
#183313=CARTESIAN_POINT('Ctrl Pts',(20.6931238587743,18.4087888131844,3.55841956124402));
#183314=CARTESIAN_POINT('Ctrl Pts',(20.6948176301499,18.4129377816118,3.55814678779655));
#183315=CARTESIAN_POINT('Ctrl Pts',(20.6978347087636,18.420395840351,3.55765852519533));
#183316=CARTESIAN_POINT('Ctrl Pts',(20.6991628401168,18.4237029067717,3.55744274853947));
#183317=CARTESIAN_POINT('Ctrl Pts',(20.7020310591701,18.4308972936601,3.55697492361436));
#183318=CARTESIAN_POINT('Ctrl Pts',(20.7035679785706,18.4347858151385,3.55672306686164));
#183319=CARTESIAN_POINT('Ctrl Pts',(20.7078539039617,18.4457242178443,3.55601733176051));
#183320=CARTESIAN_POINT('Ctrl Pts',(20.7105766793615,18.4527844030483,3.5555650024852));
#183321=CARTESIAN_POINT('Ctrl Pts',(20.7266512509448,18.495141016074,3.55286949437965));
#183322=CARTESIAN_POINT('Ctrl Pts',(20.7390960763351,18.5307770848804,3.55067700937348));
#183323=CARTESIAN_POINT('Ctrl Pts',(20.7769592981543,18.6492898371242,3.54357305343723));
#183324=CARTESIAN_POINT('Ctrl Pts',(20.7982434195186,18.7333992435162,3.5388264408764));
#183325=CARTESIAN_POINT('Ctrl Pts',(20.8469274614126,18.9914865692923,3.52453497306496));
#183326=CARTESIAN_POINT('Ctrl Pts',(20.8578578809586,19.1677608205669,3.51507770062637));
#183327=CARTESIAN_POINT('Ctrl Pts',(20.8454234299451,19.3662649488753,3.50351993292604));
#183328=CARTESIAN_POINT('Ctrl Pts',(20.8436154784559,19.3891532409696,3.50217485171648));
#183329=CARTESIAN_POINT('Ctrl Pts',(20.8405298003198,19.4215046981011,3.50025429114793));
#183330=CARTESIAN_POINT('Ctrl Pts',(20.8395597234778,19.4309960770034,3.49968846918349));
#183331=CARTESIAN_POINT('Ctrl Pts',(20.837878837021,19.4464111955738,3.4987655483667));
#183332=CARTESIAN_POINT('Ctrl Pts',(20.8372070789874,19.4523391257998,3.49840968335445));
#183333=CARTESIAN_POINT('Ctrl Pts',(20.8357481046758,19.4647449242833,3.49766290957519));
#183334=CARTESIAN_POINT('Ctrl Pts',(20.83495597707,19.4712221417209,3.49727184941826));
#183335=CARTESIAN_POINT('Ctrl Pts',(20.8329995246018,19.4866285194698,3.49633888498889));
#183336=CARTESIAN_POINT('Ctrl Pts',(20.8318081577149,19.4955540625825,3.49579613164263));
#183337=CARTESIAN_POINT('Ctrl Pts',(20.8275986363043,19.5256268633829,3.49395969721455));
#183338=CARTESIAN_POINT('Ctrl Pts',(20.8243174357203,19.546735429376,3.49265773505246));
#183339=CARTESIAN_POINT('Ctrl Pts',(20.8046822388433,19.6615735476362,3.4855015985071));
#183340=CARTESIAN_POINT('Ctrl Pts',(20.7823451858166,19.7541567335689,3.47945876524308));
#183341=CARTESIAN_POINT('Ctrl Pts',(20.7028197990833,20.0075510695226,3.46220185014897));
#183342=CARTESIAN_POINT('Ctrl Pts',(20.6323262092714,20.1634176745352,3.45070097342028));
#183343=CARTESIAN_POINT('Ctrl Pts',(20.5247189806277,20.3407713406864,3.43745842720362));
#183344=CARTESIAN_POINT('Ctrl Pts',(20.5047006626247,20.3718950410325,3.43513089479241));
#183345=CARTESIAN_POINT('Ctrl Pts',(20.479848698957,20.4083940497345,3.43241164604575));
#183346=CARTESIAN_POINT('Ctrl Pts',(20.4757918931156,20.4142876607039,3.4319728904228));
#183347=CARTESIAN_POINT('Ctrl Pts',(20.4691256952143,20.423867766163,3.43126038115275));
#183348=CARTESIAN_POINT('Ctrl Pts',(20.4665342860802,20.4275666216122,3.43098545245011));
#183349=CARTESIAN_POINT('Ctrl Pts',(20.4618754101895,20.4341714046122,3.43049487757375));
#183350=CARTESIAN_POINT('Ctrl Pts',(20.459812426369,20.4370804165301,3.43027893188099));
#183351=CARTESIAN_POINT('Ctrl Pts',(20.4553299466865,20.4433674284323,3.42981249880882));
#183352=CARTESIAN_POINT('Ctrl Pts',(20.4529078617229,20.4467435120645,3.42956219347246));
#183353=CARTESIAN_POINT('Ctrl Pts',(20.4461172525281,20.4561501775378,3.42886517455947));
#183354=CARTESIAN_POINT('Ctrl Pts',(20.4417267765237,20.4621649417681,3.42841994915767));
#183355=CARTESIAN_POINT('Ctrl Pts',(20.4161009846095,20.4968849851605,3.42585177339696));
#183356=CARTESIAN_POINT('Ctrl Pts',(20.3941725331796,20.5250743577092,3.42377410555496));
#183357=CARTESIAN_POINT('Ctrl Pts',(20.3215027755959,20.6137677138162,3.4172131149315));
#183358=CARTESIAN_POINT('Ctrl Pts',(20.2680842483836,20.6719961611282,3.4128671598357));
#183359=CARTESIAN_POINT('Ctrl Pts',(20.0773207152058,20.8579061193029,3.39834043935836));
#183360=CARTESIAN_POINT('Ctrl Pts',(19.9263513766985,20.9702903852687,3.38832616818643));
#183361=CARTESIAN_POINT('Ctrl Pts',(19.7434051941618,21.0719864758411,3.3761502372197));
#183362=CARTESIAN_POINT('Ctrl Pts',(19.7240821422682,21.0823382398379,3.37486508147468));
#183363=CARTESIAN_POINT('Ctrl Pts',(19.6971109976387,21.0962525727129,3.37307099928795));
#183364=CARTESIAN_POINT('Ctrl Pts',(19.6895967173653,21.1000725151064,3.37257113518105));
#183365=CARTESIAN_POINT('Ctrl Pts',(19.6766323688651,21.106565895805,3.37170859271869));
#183366=CARTESIAN_POINT('Ctrl Pts',(19.6711932096109,21.109260976486,3.37134667641637));
#183367=CARTESIAN_POINT('Ctrl Pts',(19.6599479645489,21.1147728360806,3.37059831377293));
#183368=CARTESIAN_POINT('Ctrl Pts',(19.6541404456095,21.1175865318348,3.37021176479006));
#183369=CARTESIAN_POINT('Ctrl Pts',(19.6405818309121,21.1240791927197,3.36930911250736));
#183370=CARTESIAN_POINT('Ctrl Pts',(19.6328210949539,21.127737658011,3.36879230482829));
#183371=CARTESIAN_POINT('Ctrl Pts',(19.6078518244859,21.1393233550017,3.36712895246425));
#183372=CARTESIAN_POINT('Ctrl Pts',(19.5905594037489,21.1470666114114,3.36597610701792));
#183373=CARTESIAN_POINT('Ctrl Pts',(19.5033261630397,21.1847307589193,3.36015446677587));
#183374=CARTESIAN_POINT('Ctrl Pts',(19.4319196699335,21.2110954369028,3.35536690731971));
#183375=CARTESIAN_POINT('Ctrl Pts',(19.2545090469346,21.2659403409532,3.34342815692353));
#183376=CARTESIAN_POINT('Ctrl Pts',(19.1474119403767,21.2901336131556,3.33617805675904));
#183377=CARTESIAN_POINT('Ctrl Pts',(18.9768280022155,21.3149634754282,3.32479162502947));
#183378=CARTESIAN_POINT('Ctrl Pts',(18.9143492319995,21.3212375516556,3.3206573973919));
#183379=CARTESIAN_POINT('Ctrl Pts',(18.8373596320936,21.3255239533143,3.31566596817692));
#183380=CARTESIAN_POINT('Ctrl Pts',(18.8230293662747,21.3261757729558,3.31474131932889));
#183381=CARTESIAN_POINT('Ctrl Pts',(18.7661724182169,21.3281830850558,3.31109280204313));
#183382=CARTESIAN_POINT('Ctrl Pts',(18.7236124982658,21.3284021685191,3.30840623374989));
#183383=CARTESIAN_POINT('Ctrl Pts',(18.6736080669189,21.3271515910924,3.30532379751994));
#183384=CARTESIAN_POINT('Ctrl Pts',(18.6661452524241,21.326925442702,3.30486570986411));
#183385=CARTESIAN_POINT('Ctrl Pts',(18.654076088554,21.3264957870548,3.30412818775641));
#183386=CARTESIAN_POINT('Ctrl Pts',(18.6494690095676,21.3263167066074,3.3038474403075));
#183387=CARTESIAN_POINT('Ctrl Pts',(18.6412909463146,21.3259720589247,3.30335051562821));
#183388=CARTESIAN_POINT('Ctrl Pts',(18.637719764109,21.3258124965392,3.30313400657374));
#183389=CARTESIAN_POINT('Ctrl Pts',(18.6300627564796,21.3254509413526,3.30267084153737));
#183390=CARTESIAN_POINT('Ctrl Pts',(18.6259771188513,21.3252461521255,3.3024243438694));
#183391=CARTESIAN_POINT('Ctrl Pts',(18.6147485609045,21.3246506966316,3.30174858745225));
#183392=CARTESIAN_POINT('Ctrl Pts',(18.6076069109588,21.3242356620749,3.30132067296169));
#183393=CARTESIAN_POINT('Ctrl Pts',(18.5692538596805,21.3218116650463,3.29903209819803));
#183394=CARTESIAN_POINT('Ctrl Pts',(18.5380859935346,21.3191473175594,3.29720596567535));
#183395=CARTESIAN_POINT('Ctrl Pts',(18.3441682524776,21.2982322516267,3.28599160251349));
#183396=CARTESIAN_POINT('Ctrl Pts',(18.1839199038445,21.2618367735806,3.27733779268349));
#183397=CARTESIAN_POINT('Ctrl Pts',(17.9189817596118,21.1683346937134,3.26195873073173));
#183398=CARTESIAN_POINT('Ctrl Pts',(17.811948499755,21.1202484320958,3.25541971901464));
#183399=CARTESIAN_POINT('Ctrl Pts',(17.6958251729989,21.0560269397287,3.24764591143057));
#183400=CARTESIAN_POINT('Ctrl Pts',(17.6822851307129,21.0483424270285,3.24672870003757));
#183401=CARTESIAN_POINT('Ctrl Pts',(17.6618321281323,21.0364343728368,3.24532617168034));
#183402=CARTESIAN_POINT('Ctrl Pts',(17.6548564343652,21.0323192353244,3.24484477588477));
#183403=CARTESIAN_POINT('Ctrl Pts',(17.6425640469567,21.0249722353528,3.2439909858391));
#183404=CARTESIAN_POINT('Ctrl Pts',(17.6372376368637,21.0217567555465,3.24361919289713));
#183405=CARTESIAN_POINT('Ctrl Pts',(17.6260012659012,21.0149057484972,3.24283094018733));
#183406=CARTESIAN_POINT('Ctrl Pts',(17.6200948595312,21.0112645584687,3.24241427518402));
#183407=CARTESIAN_POINT('Ctrl Pts',(17.6080445688555,21.0037537720816,3.24155938694752));
#183408=CARTESIAN_POINT('Ctrl Pts',(17.601902484024,20.9998814752524,3.24112106738305));
#183409=CARTESIAN_POINT('Ctrl Pts',(17.5867627192464,20.9902273627482,3.24003418996783));
#183410=CARTESIAN_POINT('Ctrl Pts',(17.5777887767252,20.9844088607213,3.23938427290224));
#183411=CARTESIAN_POINT('Ctrl Pts',(17.4713805459955,20.9142651807854,3.23160918159758));
#183412=CARTESIAN_POINT('Ctrl Pts',(17.3794004148437,20.8420647772176,3.22418040724886));
#183413=CARTESIAN_POINT('Ctrl Pts',(17.1577437695693,20.6363380216564,3.2044361289185));
#183414=CARTESIAN_POINT('Ctrl Pts',(17.0388511505898,20.4926569312126,3.19186383498346));
#183415=CARTESIAN_POINT('Ctrl Pts',(16.9326662375027,20.3232447509699,3.17941672835761));
#183416=CARTESIAN_POINT('Ctrl Pts',(16.9252264936724,20.3111046031519,3.17853708500483));
#183417=CARTESIAN_POINT('Ctrl Pts',(16.9150503854746,20.2941169173346,3.17732423590825));
#183418=CARTESIAN_POINT('Ctrl Pts',(16.9122099917785,20.2893325666758,3.17698462158532));
#183419=CARTESIAN_POINT('Ctrl Pts',(16.9076809613787,20.2816349083197,3.17644142984464));
#183420=CARTESIAN_POINT('Ctrl Pts',(16.9059803786263,20.2787287117915,3.1762370850464));
#183421=CARTESIAN_POINT('Ctrl Pts',(16.9024426117123,20.272649648161,3.17581119511931));
#183422=CARTESIAN_POINT('Ctrl Pts',(16.9006067300006,20.2694760553603,3.17558973909762));
#183423=CARTESIAN_POINT('Ctrl Pts',(16.8961856382146,20.2617875328341,3.17505531800721));
#183424=CARTESIAN_POINT('Ctrl Pts',(16.8936087875205,20.2572677735092,3.17474289135675));
#183425=CARTESIAN_POINT('Ctrl Pts',(16.8846534276858,20.2414247448557,3.17365364772372));
#183426=CARTESIAN_POINT('Ctrl Pts',(16.878362399302,20.2300520168971,3.17288224902732));
#183427=CARTESIAN_POINT('Ctrl Pts',(16.8418446088517,20.1625766114885,3.16836284648239));
#183428=CARTESIAN_POINT('Ctrl Pts',(16.8140559972057,20.1051849070304,3.16475095998148));
#183429=CARTESIAN_POINT('Ctrl Pts',(16.7733771411984,20.0104954526878,3.15902267577751));
#183430=CARTESIAN_POINT('Ctrl Pts',(16.7588808356048,19.9739768425109,3.15686676387554));
#183431=CARTESIAN_POINT('Ctrl Pts',(16.7454192904822,19.9371100204058,3.15472448980525));
#183432=CARTESIAN_POINT('Ctrl Pts',(16.7454193815904,19.9371102699218,2.93545674419276));
#183433=CARTESIAN_POINT('Ctrl Pts',(16.7888438165966,20.0560357188456,2.9427087427267));
#183434=CARTESIAN_POINT('Ctrl Pts',(16.842869814061,20.1708827553276,2.94951932184116));
#183435=CARTESIAN_POINT('Ctrl Pts',(16.9474347316042,20.3495612776988,2.9607700351766));
#183436=CARTESIAN_POINT('Ctrl Pts',(16.9919020020283,20.4165002381309,2.96515171230137));
#183437=CARTESIAN_POINT('Ctrl Pts',(17.0691830410257,20.5195988133736,2.97235633827638));
#183438=CARTESIAN_POINT('Ctrl Pts',(17.0996305576116,20.5574332223459,2.97510777916505));
#183439=CARTESIAN_POINT('Ctrl Pts',(17.1516600481911,20.6177179978778,2.97970139741259));
#183440=CARTESIAN_POINT('Ctrl Pts',(17.1724847726145,20.6407990403733,2.98151393278074));
#183441=CARTESIAN_POINT('Ctrl Pts',(17.2008236769895,20.6708506399273,2.98395107201981));
#183442=CARTESIAN_POINT('Ctrl Pts',(17.2078917018916,20.6782378761561,2.98455657376902));
#183443=CARTESIAN_POINT('Ctrl Pts',(17.2198177092573,20.690523090417,2.98557450218282));
#183444=CARTESIAN_POINT('Ctrl Pts',(17.2246466703181,20.6954490928025,2.98598566080853));
#183445=CARTESIAN_POINT('Ctrl Pts',(17.2340420891884,20.7049400779573,2.9867837288943));
#183446=CARTESIAN_POINT('Ctrl Pts',(17.2386055310559,20.7095079484448,2.98717050298134));
#183447=CARTESIAN_POINT('Ctrl Pts',(17.2491925704219,20.7200087408093,2.98806588421118));
#183448=CARTESIAN_POINT('Ctrl Pts',(17.2552309254785,20.7259265671207,2.98857514749535));
#183449=CARTESIAN_POINT('Ctrl Pts',(17.2715701678263,20.7417488988815,2.98994946803813));
#183450=CARTESIAN_POINT('Ctrl Pts',(17.2819360220103,20.751585406125,2.99081745344438));
#183451=CARTESIAN_POINT('Ctrl Pts',(17.3779765191944,20.8408910269106,2.99882522204315));
#183452=CARTESIAN_POINT('Ctrl Pts',(17.4699800068057,20.9132309151536,3.00626682640924));
#183453=CARTESIAN_POINT('Ctrl Pts',(17.7032741064157,21.0672808535762,3.02452801992163));
#183454=CARTESIAN_POINT('Ctrl Pts',(17.8489648297749,21.1409967095266,3.03548771682661));
#183455=CARTESIAN_POINT('Ctrl Pts',(18.0321397643256,21.2085325933386,3.0478926931446));
#183456=CARTESIAN_POINT('Ctrl Pts',(18.0628753890759,21.2190677967933,3.04992865328473));
#183457=CARTESIAN_POINT('Ctrl Pts',(18.1007423661343,21.2310807306317,3.05237155595379));
#183458=CARTESIAN_POINT('Ctrl Pts',(18.1076528430853,21.2332340694463,3.05281473115043));
#183459=CARTESIAN_POINT('Ctrl Pts',(18.1185038250503,21.2365543303391,3.05350633405705));
#183460=CARTESIAN_POINT('Ctrl Pts',(18.1224368393167,21.2377452695619,3.05375613172592));
#183461=CARTESIAN_POINT('Ctrl Pts',(18.1297949762233,21.2399499865597,3.05422179533168));
#183462=CARTESIAN_POINT('Ctrl Pts',(18.1332191590904,21.2409665367053,3.05443781659813));
#183463=CARTESIAN_POINT('Ctrl Pts',(18.1410416518625,21.2432673029967,3.05492977965259));
#183464=CARTESIAN_POINT('Ctrl Pts',(18.1454415598256,21.244545907242,3.05520539208649));
#183465=CARTESIAN_POINT('Ctrl Pts',(18.1589788682761,21.2484322047206,3.0560500916804));
#183466=CARTESIAN_POINT('Ctrl Pts',(18.1681298472089,21.2509927128683,3.05661650285559));
#183467=CARTESIAN_POINT('Ctrl Pts',(18.2505207023821,21.2734491864912,3.06167757166063));
#183468=CARTESIAN_POINT('Ctrl Pts',(18.3247723504347,21.2894571714883,3.06596582529913));
#183469=CARTESIAN_POINT('Ctrl Pts',(18.549793353905,21.3254387841469,3.0785782444002));
#183470=CARTESIAN_POINT('Ctrl Pts',(18.7020030680415,21.3332069250289,3.08663340571346));
#183471=CARTESIAN_POINT('Ctrl Pts',(18.9087591576203,21.321494113719,3.09814821965788));
#183472=CARTESIAN_POINT('Ctrl Pts',(18.9636353790275,21.3162299433859,3.10125575987805));
#183473=CARTESIAN_POINT('Ctrl Pts',(19.0522382603209,21.3042248893456,3.10639980685562));
#183474=CARTESIAN_POINT('Ctrl Pts',(19.086116913803,21.2987929758776,3.10839692523103));
#183475=CARTESIAN_POINT('Ctrl Pts',(19.1304751697484,21.2905704539348,3.11105757975755));
#183476=CARTESIAN_POINT('Ctrl Pts',(19.1410876609821,21.2885190643706,3.11169758741297));
#183477=CARTESIAN_POINT('Ctrl Pts',(19.1584464133113,21.2850255126441,3.11275029581444));
#183478=CARTESIAN_POINT('Ctrl Pts',(19.1652022408267,21.2836314700511,3.11316145526646));
#183479=CARTESIAN_POINT('Ctrl Pts',(19.1782682275935,21.2808686993638,3.1139595238048));
#183480=CARTESIAN_POINT('Ctrl Pts',(19.1845791825267,21.2795040704567,3.11434629751201));
#183481=CARTESIAN_POINT('Ctrl Pts',(19.1991392101263,21.2762859359822,3.11524167618479));
#183482=CARTESIAN_POINT('Ctrl Pts',(19.2073835778841,21.2744118510644,3.11575093728024));
#183483=CARTESIAN_POINT('Ctrl Pts',(19.2295316229063,21.2692375015141,3.11712524811891));
#183484=CARTESIAN_POINT('Ctrl Pts',(19.2434132902838,21.2658458058707,3.1179932259456));
#183485=CARTESIAN_POINT('Ctrl Pts',(19.3704809799966,21.2334327510907,3.12600041891884));
#183486=CARTESIAN_POINT('Ctrl Pts',(19.4810985669252,21.195232394466,3.13344140493276));
#183487=CARTESIAN_POINT('Ctrl Pts',(19.7368748262521,21.0824719579531,3.1517000702034));
#183488=CARTESIAN_POINT('Ctrl Pts',(19.8776957779812,20.9998893889129,3.16265778499397));
#183489=CARTESIAN_POINT('Ctrl Pts',(20.0336423808164,20.8824293663801,3.17506348767464));
#183490=CARTESIAN_POINT('Ctrl Pts',(20.0591645165765,20.862267912132,3.17710161022173));
#183491=CARTESIAN_POINT('Ctrl Pts',(20.089790084121,20.8369073375529,3.17954674175958));
#183492=CARTESIAN_POINT('Ctrl Pts',(20.0953429998953,20.832260824986,3.17999005981816));
#183493=CARTESIAN_POINT('Ctrl Pts',(20.1040104120163,20.8249322667531,3.18068183581329));
#183494=CARTESIAN_POINT('Ctrl Pts',(20.1071410616139,20.8222695355754,3.18093166481558));
#183495=CARTESIAN_POINT('Ctrl Pts',(20.1129780390042,20.8172756071552,3.18139735556651));
#183496=CARTESIAN_POINT('Ctrl Pts',(20.1156861914198,20.8149467032504,3.18161337283364));
#183497=CARTESIAN_POINT('Ctrl Pts',(20.1218543161038,20.8096151455945,3.18210528630179));
#183498=CARTESIAN_POINT('Ctrl Pts',(20.1253104376405,20.8066081140022,3.18238085340561));
#183499=CARTESIAN_POINT('Ctrl Pts',(20.1359022115561,20.7973320604515,3.18322527600377));
#183500=CARTESIAN_POINT('Ctrl Pts',(20.1430055698759,20.7910261163809,3.18379145806017));
#183501=CARTESIAN_POINT('Ctrl Pts',(20.2063661541298,20.734011205562,3.1888430881696));
#183502=CARTESIAN_POINT('Ctrl Pts',(20.2599132867403,20.680359199217,3.19312298397862));
#183503=CARTESIAN_POINT('Ctrl Pts',(20.339024856642,20.592091623838,3.19968395834863));
#183504=CARTESIAN_POINT('Ctrl Pts',(20.3666040791301,20.5593779038406,3.20202237579589));
#183505=CARTESIAN_POINT('Ctrl Pts',(20.4610725903443,20.4401706605752,3.21030324339247));
#183506=CARTESIAN_POINT('Ctrl Pts',(20.5222319092832,20.3493611012446,3.21618996196601));
#183507=CARTESIAN_POINT('Ctrl Pts',(20.6032437751801,20.2063140731562,3.22533110955767));
#183508=CARTESIAN_POINT('Ctrl Pts',(20.6285026711613,20.1573516153469,3.2284367983729));
#183509=CARTESIAN_POINT('Ctrl Pts',(20.6663441304474,20.076396514243,3.23357805384042));
#183510=CARTESIAN_POINT('Ctrl Pts',(20.6801078982327,20.0449837033386,3.23557428814808));
#183511=CARTESIAN_POINT('Ctrl Pts',(20.6971975823155,20.003250621606,3.23823393176517));
#183512=CARTESIAN_POINT('Ctrl Pts',(20.7012163274404,19.9932184535927,3.23887383539348));
#183513=CARTESIAN_POINT('Ctrl Pts',(20.7076739312553,19.9767334997025,3.23992641627247));
#183514=CARTESIAN_POINT('Ctrl Pts',(20.7101584072572,19.9702987074785,3.24033755296232));
#183515=CARTESIAN_POINT('Ctrl Pts',(20.7149076159217,19.9578170524806,3.24113560847535));
#183516=CARTESIAN_POINT('Ctrl Pts',(20.717176221123,19.9517717376032,3.24152239208429));
#183517=CARTESIAN_POINT('Ctrl Pts',(20.7223517018704,19.9377860813852,3.24241783907507));
#183518=CARTESIAN_POINT('Ctrl Pts',(20.7252387172747,19.9298385535096,3.24292715890185));
#183519=CARTESIAN_POINT('Ctrl Pts',(20.7328775826639,19.9084107156541,3.24430173100157));
#183520=CARTESIAN_POINT('Ctrl Pts',(20.7375405874086,19.8948994046376,3.24516991309015));
#183521=CARTESIAN_POINT('Ctrl Pts',(20.7791461011179,19.7702665896041,3.25319285228735));
#183522=CARTESIAN_POINT('Ctrl Pts',(20.8069399457499,19.6563243978833,3.2606507587467));
#183523=CARTESIAN_POINT('Ctrl Pts',(20.850637683637,19.3791524371772,3.27898078895461));
#183524=CARTESIAN_POINT('Ctrl Pts',(20.8573023189426,19.2152173779122,3.2899950743259));
#183525=CARTESIAN_POINT('Ctrl Pts',(20.8426631836432,19.0206710324036,3.30238089400103));
#183526=CARTESIAN_POINT('Ctrl Pts',(20.8395905040362,18.9892469513951,3.30435813089164));
#183527=CARTESIAN_POINT('Ctrl Pts',(20.834958191279,18.950778653771,3.30674040830874));
#183528=CARTESIAN_POINT('Ctrl Pts',(20.8340642497277,18.943660102215,3.30717963553787));
#183529=CARTESIAN_POINT('Ctrl Pts',(20.8326031973522,18.9324853836982,3.30786645376848));
#183530=CARTESIAN_POINT('Ctrl Pts',(20.8320604846544,18.928426160412,3.30811538428804));
#183531=CARTESIAN_POINT('Ctrl Pts',(20.8310220832004,18.9208273680417,3.30858030213779));
#183532=CARTESIAN_POINT('Ctrl Pts',(20.8305292158416,18.9172875196588,3.30879643955997));
#183533=CARTESIAN_POINT('Ctrl Pts',(20.8293810128716,18.909191117324,3.30928979997919));
#183534=CARTESIAN_POINT('Ctrl Pts',(20.828719779366,18.9046354498058,3.30956668640284));
#183535=CARTESIAN_POINT('Ctrl Pts',(20.8269506547889,18.892720336281,3.31028907731625));
#183536=CARTESIAN_POINT('Ctrl Pts',(20.8258187953795,18.8853644388208,3.31073326151981));
#183537=CARTESIAN_POINT('Ctrl Pts',(20.8180275874156,18.8364473642736,3.31367609690752));
#183538=CARTESIAN_POINT('Ctrl Pts',(20.8101683034888,18.7950836971355,3.31611160469689));
#183539=CARTESIAN_POINT('Ctrl Pts',(20.7652809927486,18.592060953506,3.32792429780905));
#183540=CARTESIAN_POINT('Ctrl Pts',(20.7105787554934,18.4348978885238,3.33666241121533));
#183541=CARTESIAN_POINT('Ctrl Pts',(20.5968915197295,18.2009466375424,3.35097834868492));
#183542=CARTESIAN_POINT('Ctrl Pts',(20.5500855008844,18.1190278970036,3.35626638273926));
#183543=CARTESIAN_POINT('Ctrl Pts',(20.4862296072675,18.0227945539469,3.36299242362801));
#183544=CARTESIAN_POINT('Ctrl Pts',(20.474211886118,18.005262333014,3.36423973092433));
#183545=CARTESIAN_POINT('Ctrl Pts',(20.4567405101453,17.9805793826487,3.366028640662));
#183546=CARTESIAN_POINT('Ctrl Pts',(20.4515018963831,17.9732774975678,3.3665620203287));
#183547=CARTESIAN_POINT('Ctrl Pts',(20.4423813400599,17.9607341337148,3.3674856091723));
#183548=CARTESIAN_POINT('Ctrl Pts',(20.4385213458098,17.9554767944505,3.36787496513259));
#183549=CARTESIAN_POINT('Ctrl Pts',(20.4310819709702,17.9454418541281,3.36862250979981));
#183550=CARTESIAN_POINT('Ctrl Pts',(20.4275065508397,17.94066138455,3.36898054142496));
#183551=CARTESIAN_POINT('Ctrl Pts',(20.4181518870015,17.9282635323524,3.36991410798059));
#183552=CARTESIAN_POINT('Ctrl Pts',(20.4123412186485,17.9206701301538,3.37049087620771));
#183553=CARTESIAN_POINT('Ctrl Pts',(20.3923265260562,17.8948787864966,3.37246716158348));
#183554=CARTESIAN_POINT('Ctrl Pts',(20.3778767688503,17.8768744368385,3.37387641519409));
#183555=CARTESIAN_POINT('Ctrl Pts',(20.2518700904684,17.7250262209856,3.38602298372876));
#183556=CARTESIAN_POINT('Ctrl Pts',(20.1244962580515,17.6052151820562,3.39745268855204));
#183557=CARTESIAN_POINT('Ctrl Pts',(19.912987640556,17.4504881924912,3.41476834823958));
#183558=CARTESIAN_POINT('Ctrl Pts',(19.8388846301562,17.4030604063571,3.42056300459969));
#183559=CARTESIAN_POINT('Ctrl Pts',(19.7287863473539,17.3418995489147,3.42860559252335));
#183560=CARTESIAN_POINT('Ctrl Pts',(19.695034526667,17.3243231785901,3.43099903614493));
#183561=CARTESIAN_POINT('Ctrl Pts',(19.6540061279172,17.3043444866022,3.43380724197334));
#183562=CARTESIAN_POINT('Ctrl Pts',(19.647169350151,17.3010606648069,3.43427187573751));
#183563=CARTESIAN_POINT('Ctrl Pts',(19.6365328792941,17.2960219542045,3.43498944221276));
#183564=CARTESIAN_POINT('Ctrl Pts',(19.6327454618046,17.2942415098216,3.43524391533606));
#183565=CARTESIAN_POINT('Ctrl Pts',(19.6257233363084,17.2909658362382,3.43571377399474));
#183566=CARTESIAN_POINT('Ctrl Pts',(19.622490160452,17.2894675559306,3.43592934266991));
#183567=CARTESIAN_POINT('Ctrl Pts',(19.615186898773,17.2861055385664,3.43641456369887));
#183568=CARTESIAN_POINT('Ctrl Pts',(19.6111146874282,17.2842465481617,3.43668392223838));
#183569=CARTESIAN_POINT('Ctrl Pts',(19.5991211358053,17.2788173188329,3.43747382049991));
#183570=CARTESIAN_POINT('Ctrl Pts',(19.5911835665603,17.275282863615,3.43799221431717));
#183571=CARTESIAN_POINT('Ctrl Pts',(19.5351571805879,17.2507475382872,3.44162204726622));
#183572=CARTESIAN_POINT('Ctrl Pts',(19.4863196592021,17.2314903013438,3.4446354357532));
#183573=CARTESIAN_POINT('Ctrl Pts',(19.4341006648784,17.2131120337244,3.44775095004734));
#183574=CARTESIAN_POINT('Ctrl Pts',(19.4313865855177,17.2121630338578,3.44791257927123));
#183575=CARTESIAN_POINT('Ctrl Pts',(19.289263182848,17.1627931413185,3.45636107009442));
#183576=CARTESIAN_POINT('Ctrl Pts',(19.145167404338,17.1290740964683,3.46418617869217));
#183577=CARTESIAN_POINT('Ctrl Pts',(18.9017617407453,17.0983957175669,3.47766680584885));
#183578=CARTESIAN_POINT('Ctrl Pts',(18.8040761375589,17.0929048787396,3.48313954024638));
#183579=CARTESIAN_POINT('Ctrl Pts',(18.6847008455892,17.0944631785398,3.49008936849941));
#183580=CARTESIAN_POINT('Ctrl Pts',(18.6630404484748,17.0950786370934,3.49136057142821));
#183581=CARTESIAN_POINT('Ctrl Pts',(18.6323461929285,17.0964226140365,3.4931778207493));
#183582=CARTESIAN_POINT('Ctrl Pts',(18.6233012429599,17.09687682501,3.49371527921302));
#183583=CARTESIAN_POINT('Ctrl Pts',(18.60773510642,17.0977586786699,3.49464370211374));
#183584=CARTESIAN_POINT('Ctrl Pts',(18.6012124251245,17.0981585094925,3.49503378913057));
#183585=CARTESIAN_POINT('Ctrl Pts',(18.5887492823287,17.0989804225382,3.49578119034145));
#183586=CARTESIAN_POINT('Ctrl Pts',(18.5828085370981,17.0993973842161,3.49613833999094));
#183587=CARTESIAN_POINT('Ctrl Pts',(18.5674132512408,17.1005432308385,3.49706622752736));
#183588=CARTESIAN_POINT('Ctrl Pts',(18.5579617840153,17.101310577052,3.49763816916063));
#183589=CARTESIAN_POINT('Ctrl Pts',(18.525997458932,17.1041219906394,3.49958037701081));
#183590=CARTESIAN_POINT('Ctrl Pts',(18.5035128963335,17.1064630826981,3.50095993055254));
#183591=CARTESIAN_POINT('Ctrl Pts',(18.3020350935236,17.1307083678691,3.51344598240394));
#183592=CARTESIAN_POINT('Ctrl Pts',(18.1265177986523,17.1750366007595,3.52530095125202));
#183593=CARTESIAN_POINT('Ctrl Pts',(17.880919245885,17.2716847736613,3.54273407999321));
#183594=CARTESIAN_POINT('Ctrl Pts',(17.8049370367176,17.3069164525899,3.54824059718542));
#183595=CARTESIAN_POINT('Ctrl Pts',(17.6986806013986,17.3640649292396,3.55593786556592));
#183596=CARTESIAN_POINT('Ctrl Pts',(17.6665872811858,17.3824251764925,3.55826173456031));
#183597=CARTESIAN_POINT('Ctrl Pts',(17.6285601012713,17.4055227191648,3.56099931786265));
#183598=CARTESIAN_POINT('Ctrl Pts',(17.6221518101811,17.4094619937365,3.56146009139507));
#183599=CARTESIAN_POINT('Ctrl Pts',(17.6122225237722,17.4156388400008,3.56217299284663));
#183600=CARTESIAN_POINT('Ctrl Pts',(17.6086869903064,17.4178527578826,3.56242662989085));
#183601=CARTESIAN_POINT('Ctrl Pts',(17.6021423738702,17.4219779148723,3.5628957184863));
#183602=CARTESIAN_POINT('Ctrl Pts',(17.5991316014956,17.4238862864196,3.56311134825268));
#183603=CARTESIAN_POINT('Ctrl Pts',(17.5923358773359,17.4282178406188,3.56359768455261));
#183604=CARTESIAN_POINT('Ctrl Pts',(17.5885538231774,17.4306454696761,3.56386809129828));
#183605=CARTESIAN_POINT('Ctrl Pts',(17.5774135313311,17.4378464061516,3.56466392390217));
#183606=CARTESIAN_POINT('Ctrl Pts',(17.5700770904319,17.4426534860251,3.56518715528834));
#183607=CARTESIAN_POINT('Ctrl Pts',(17.5172400435089,17.4777453588312,3.56895081489696));
#183608=CARTESIAN_POINT('Ctrl Pts',(17.4728934029473,17.5097393842686,3.5720847551078));
#183609=CARTESIAN_POINT('Ctrl Pts',(17.297250717459,17.6471044830489,3.58461109107506));
#183610=CARTESIAN_POINT('Ctrl Pts',(17.17750277928,17.7662364824458,3.59346953724732));
#183611=CARTESIAN_POINT('Ctrl Pts',(17.0365790409051,17.9445386110824,3.60606881828863));
#183612=CARTESIAN_POINT('Ctrl Pts',(17.001983831978,17.9922787063494,3.60938273608767));
#183613=CARTESIAN_POINT('Ctrl Pts',(16.9495309651219,18.0714140607528,3.61483688368836));
#183614=CARTESIAN_POINT('Ctrl Pts',(16.9304052176692,18.1019321552546,3.61693119722609));
#183615=CARTESIAN_POINT('Ctrl Pts',(16.9064660224197,18.1423889545513,3.61970280990592));
#183616=CARTESIAN_POINT('Ctrl Pts',(16.9009381182918,18.1518993737209,3.62035400213238));
#183617=CARTESIAN_POINT('Ctrl Pts',(16.8920438745124,18.1674796124726,3.62142042870922));
#183618=CARTESIAN_POINT('Ctrl Pts',(16.888632778462,18.1735237432517,3.62183404219457));
#183619=CARTESIAN_POINT('Ctrl Pts',(16.8821134430049,18.1852092487347,3.62263358139292));
#183620=CARTESIAN_POINT('Ctrl Pts',(16.879001103691,18.1908482570564,3.62301935422731));
#183621=CARTESIAN_POINT('Ctrl Pts',(16.8719106580075,18.2038346258148,3.62390768443774));
#183622=CARTESIAN_POINT('Ctrl Pts',(16.8679502372614,18.2111914741425,3.62441086542054));
#183623=CARTESIAN_POINT('Ctrl Pts',(16.8574948764112,18.2308918094754,3.62575822270598));
#183624=CARTESIAN_POINT('Ctrl Pts',(16.8510782839663,18.2432762064191,3.62660515107105));
#183625=CARTESIAN_POINT('Ctrl Pts',(16.800137530275,18.3440198034776,3.633495157055));
#183626=CARTESIAN_POINT('Ctrl Pts',(16.7617417211774,18.4353253610798,3.63975148057327));
#183627=CARTESIAN_POINT('Ctrl Pts',(16.6860055179091,18.6578740565154,3.65499319268893));
#183628=CARTESIAN_POINT('Ctrl Pts',(16.6546777558883,18.7907082759852,3.66409684657822));
#183629=CARTESIAN_POINT('Ctrl Pts',(16.6262468700561,18.9996860794504,3.67787830996548));
#183630=CARTESIAN_POINT('Ctrl Pts',(16.6200989475176,19.0742460100602,3.68268510272746));
#183631=CARTESIAN_POINT('Ctrl Pts',(16.6176490858976,19.1578371891601,3.68784414803085));
#183632=CARTESIAN_POINT('Ctrl Pts',(16.6174451480605,19.1666937802207,3.68838785452539));
#183633=CARTESIAN_POINT('Ctrl Pts',(16.6172222390665,19.1800041618254,3.68920035751529));
#183634=CARTESIAN_POINT('Ctrl Pts',(16.6171617202339,19.1844570287512,3.68947139586155));
#183635=CARTESIAN_POINT('Ctrl Pts',(16.6170816555811,19.1921296594547,3.68993703801595));
#183636=CARTESIAN_POINT('Ctrl Pts',(16.6170554039638,19.1953492978433,3.69013201417728));
#183637=CARTESIAN_POINT('Ctrl Pts',(16.6170125976395,19.2026391212519,3.69057251818924));
#183638=CARTESIAN_POINT('Ctrl Pts',(16.617000435401,19.2067092918388,3.69081779729758));
#183639=CARTESIAN_POINT('Ctrl Pts',(16.6169992761378,19.2178398538869,3.69148678276288));
#183640=CARTESIAN_POINT('Ctrl Pts',(16.6170338608861,19.2249002690473,3.69190918932611));
#183641=CARTESIAN_POINT('Ctrl Pts',(16.6174008065008,19.2619597899229,3.69411674934474));
#183642=CARTESIAN_POINT('Ctrl Pts',(16.6183355257014,19.2919511380406,3.69587020382201));
#183643=CARTESIAN_POINT('Ctrl Pts',(16.6230423747871,19.3816665828137,3.7010431490907));
#183644=CARTESIAN_POINT('Ctrl Pts',(16.6287093229192,19.4412636993934,3.70438374006535));
#183645=CARTESIAN_POINT('Ctrl Pts',(16.6574679249874,19.6495557923784,3.7159609047263));
#183646=CARTESIAN_POINT('Ctrl Pts',(16.693857304765,19.7958984467168,3.72394888923627));
#183647=CARTESIAN_POINT('Ctrl Pts',(16.7454193623262,19.9371102171632,3.73234496441554));
#183648=CARTESIAN_POINT('Origin',(18.734,19.211,0.));
#183649=CARTESIAN_POINT('',(16.745419360568,19.9371102123481,4.75730092050388));
#183650=CARTESIAN_POINT('',(16.7454193895773,19.9371102917951,4.53222340700496));
#183651=CARTESIAN_POINT('',(16.7454193623258,19.9371102171621,0.));
#183652=CARTESIAN_POINT('',(16.6170000778091,19.2104260280332,4.70909169803339));
#183653=CARTESIAN_POINT('Ctrl Pts',(16.745419360568,19.9371102123481,4.75730092050388));
#183654=CARTESIAN_POINT('Ctrl Pts',(16.7278325677703,19.8889456843294,4.7540835371879));
#183655=CARTESIAN_POINT('Ctrl Pts',(16.7120013965261,19.8401580434368,4.75081295266123));
#183656=CARTESIAN_POINT('Ctrl Pts',(16.6441871892237,19.6020374009016,4.73481653533855));
#183657=CARTESIAN_POINT('Ctrl Pts',(16.6169468631223,19.4066995299123,4.72148364047144));
#183658=CARTESIAN_POINT('Ctrl Pts',(16.6170000778091,19.2104260280332,4.70909169803339));
#183659=CARTESIAN_POINT('Ctrl Pts',(16.6170000784465,19.2104236820643,4.70909154991813));
#183660=CARTESIAN_POINT('Ctrl Pts',(16.6170043637984,19.1946822152069,4.7080976958813));
#183661=CARTESIAN_POINT('Ctrl Pts',(16.61718422352,19.1789407204702,4.70711096664662));
#183662=CARTESIAN_POINT('Ctrl Pts',(16.6177851446148,19.1523322925812,4.70545671999246));
#183663=CARTESIAN_POINT('Ctrl Pts',(16.6181143693901,19.1414642294231,4.70478490712336));
#183664=CARTESIAN_POINT('Ctrl Pts',(16.6187085002863,19.1258317544558,4.70382459025789));
#183665=CARTESIAN_POINT('Ctrl Pts',(16.6189057981698,19.1210651502801,4.70353257788567));
#183666=CARTESIAN_POINT('Ctrl Pts',(16.6192791186639,19.1127280680581,4.70302328572276));
#183667=CARTESIAN_POINT('Ctrl Pts',(16.6194480743017,19.1091573148174,4.70280562422508));
#183668=CARTESIAN_POINT('Ctrl Pts',(16.6197955283655,19.1021880828528,4.7023817372304));
#183669=CARTESIAN_POINT('Ctrl Pts',(16.6199731789515,19.0987895650075,4.70217546500797));
#183670=CARTESIAN_POINT('Ctrl Pts',(16.6203449449137,19.0919920226564,4.70176377589654));
#183671=CARTESIAN_POINT('Ctrl Pts',(16.620539064392,19.0885930369605,4.70155835900012));
#183672=CARTESIAN_POINT('Ctrl Pts',(16.6210263189945,19.0804082195942,4.7010647413133));
#183673=CARTESIAN_POINT('Ctrl Pts',(16.6213275168543,19.0756228611888,4.70077698963592));
#183674=CARTESIAN_POINT('Ctrl Pts',(16.6224923818642,19.0580673362408,4.69972432499825));
#183675=CARTESIAN_POINT('Ctrl Pts',(16.6234556168969,19.045303753542,4.69896478033461));
#183676=CARTESIAN_POINT('Ctrl Pts',(16.6267051775263,19.0068906935396,4.69669420547832));
#183677=CARTESIAN_POINT('Ctrl Pts',(16.629343849213,18.9812725791769,4.695200552628));
#183678=CARTESIAN_POINT('Ctrl Pts',(16.6544361109332,18.7747145114139,4.68327865541669));
#183679=CARTESIAN_POINT('Ctrl Pts',(16.6997133937434,18.5973029667728,4.67373447942496));
#183680=CARTESIAN_POINT('Ctrl Pts',(16.7997460845995,18.3460701586725,4.65880486824974));
#183681=CARTESIAN_POINT('Ctrl Pts',(16.837386179554,18.2663861571441,4.6538477966998));
#183682=CARTESIAN_POINT('Ctrl Pts',(16.8897666853855,18.1713305359165,4.6475220897332));
#183683=CARTESIAN_POINT('Ctrl Pts',(16.8999188137765,18.1535241033014,4.64631864737917));
#183684=CARTESIAN_POINT('Ctrl Pts',(16.9148254325188,18.1282390247297,4.64458188054752));
#183685=CARTESIAN_POINT('Ctrl Pts',(16.9193710093483,18.1206381063182,4.64405612911386));
#183686=CARTESIAN_POINT('Ctrl Pts',(16.9273346985559,18.1075092992296,4.64314154097948));
#183687=CARTESIAN_POINT('Ctrl Pts',(16.9307308433286,18.1019681766182,4.64275351260169));
#183688=CARTESIAN_POINT('Ctrl Pts',(16.9373104942306,18.0913429982608,4.64200553083691));
#183689=CARTESIAN_POINT('Ctrl Pts',(16.9404902033203,18.0862566560551,4.64164572019096));
#183690=CARTESIAN_POINT('Ctrl Pts',(16.9488782202422,18.0729649895568,4.64070083322307));
#183691=CARTESIAN_POINT('Ctrl Pts',(16.9541214456695,18.0647819664361,4.6401144641528));
#183692=CARTESIAN_POINT('Ctrl Pts',(16.972522401082,18.0364945825453,4.63807108359136));
#183693=CARTESIAN_POINT('Ctrl Pts',(16.9859655294557,18.0165789175181,4.63660342561447));
#183694=CARTESIAN_POINT('Ctrl Pts',(17.0837213670924,17.8769419853157,4.62610101572627));
#183695=CARTESIAN_POINT('Ctrl Pts',(17.179902504675,17.7660441907809,4.61659536390066));
#183696=CARTESIAN_POINT('Ctrl Pts',(17.3663203626474,17.591421911081,4.59973664771492));
#183697=CARTESIAN_POINT('Ctrl Pts',(17.4515512190127,17.5231291555232,4.59248962796451));
#183698=CARTESIAN_POINT('Ctrl Pts',(17.5653061675201,17.4455929327199,4.58366375732444));
#183699=CARTESIAN_POINT('Ctrl Pts',(17.5892701213525,17.4299606816151,4.5818487576108));
#183700=CARTESIAN_POINT('Ctrl Pts',(17.6237470527143,17.4084540271461,4.57930746203041));
#183701=CARTESIAN_POINT('Ctrl Pts',(17.6340037024147,17.4021766943717,4.57856003645289));
#183702=CARTESIAN_POINT('Ctrl Pts',(17.6498689037046,17.3926516416282,4.57741771911225));
#183703=CARTESIAN_POINT('Ctrl Pts',(17.655439637811,17.3893418174921,4.5770192118189));
#183704=CARTESIAN_POINT('Ctrl Pts',(17.6646954088453,17.3838998892428,4.57636149151379));
#183705=CARTESIAN_POINT('Ctrl Pts',(17.6683717933226,17.3817532563253,4.57610138842673));
#183706=CARTESIAN_POINT('Ctrl Pts',(17.6755037846931,17.3776176998128,4.57559904941793));
#183707=CARTESIAN_POINT('Ctrl Pts',(17.6789585811857,17.3756274215703,4.5753567281989));
#183708=CARTESIAN_POINT('Ctrl Pts',(17.6854556785708,17.3719089071104,4.57490295328743));
#183709=CARTESIAN_POINT('Ctrl Pts',(17.6884966058051,17.3701784728348,4.57469136268995));
#183710=CARTESIAN_POINT('Ctrl Pts',(17.6955301546883,17.3661990952099,4.57420378054315));
#183711=CARTESIAN_POINT('Ctrl Pts',(17.6995257914741,17.3639555742385,4.57392813911222));
#183712=CARTESIAN_POINT('Ctrl Pts',(17.7118313607079,17.3570985433665,4.57308326245629));
#183713=CARTESIAN_POINT('Ctrl Pts',(17.7201652351334,17.3525279353114,4.57251670484441));
#183714=CARTESIAN_POINT('Ctrl Pts',(17.8341057564339,17.2910332323665,4.5648432674565));
#183715=CARTESIAN_POINT('Ctrl Pts',(17.9443507123299,17.2431218460717,4.55825736830397));
#183716=CARTESIAN_POINT('Ctrl Pts',(18.1612061090215,17.1700591808931,4.5458024745412));
#183717=CARTESIAN_POINT('Ctrl Pts',(18.2668613705971,17.1433170391643,4.53993996763126));
#183718=CARTESIAN_POINT('Ctrl Pts',(18.4478899559138,17.1120866870742,4.52972021388724));
#183719=CARTESIAN_POINT('Ctrl Pts',(18.5222968787215,17.1032817678786,4.52547353616279));
#183720=CARTESIAN_POINT('Ctrl Pts',(18.6157555105095,17.0972213564375,4.52000497375922));
#183721=CARTESIAN_POINT('Ctrl Pts',(18.6345170069107,17.096255331323,4.51890059880665));
#183722=CARTESIAN_POINT('Ctrl Pts',(18.6618325982199,17.0952131546314,4.51728219362356));
#183723=CARTESIAN_POINT('Ctrl Pts',(18.6703785558973,17.0949389381465,4.51677436661677));
#183724=CARTESIAN_POINT('Ctrl Pts',(18.6853723407897,17.0945487399419,4.51588068232854));
#183725=CARTESIAN_POINT('Ctrl Pts',(18.6918195127689,17.0944104340902,4.51549552961081));
#183726=CARTESIAN_POINT('Ctrl Pts',(18.7043451869666,17.0941989831386,4.5147455051637));
#183727=CARTESIAN_POINT('Ctrl Pts',(18.7104235761975,17.0941225581145,4.51438074014408));
#183728=CARTESIAN_POINT('Ctrl Pts',(18.7249640896626,17.0940023709399,4.51350621890186));
#183729=CARTESIAN_POINT('Ctrl Pts',(18.7334262632324,17.0939831657035,4.51299569770762));
#183730=CARTESIAN_POINT('Ctrl Pts',(18.7640159917895,17.0940971479788,4.51114440738714));
#183731=CARTESIAN_POINT('Ctrl Pts',(18.7861404089094,17.094526526485,4.50979441237954));
#183732=CARTESIAN_POINT('Ctrl Pts',(18.9935807666004,17.1018069392241,4.4970291282802));
#183733=CARTESIAN_POINT('Ctrl Pts',(19.1772172861537,17.1326332277532,4.48481601825516));
#183734=CARTESIAN_POINT('Ctrl Pts',(19.4311711120825,17.2104796833393,4.46727914861177));
#183735=CARTESIAN_POINT('Ctrl Pts',(19.5065033666126,17.238344590235,4.46200621723894));
#183736=CARTESIAN_POINT('Ctrl Pts',(19.6131283199232,17.2848321621284,4.45459117425866));
#183737=CARTESIAN_POINT('Ctrl Pts',(19.6458097224811,17.3000859434502,4.45232574053615));
#183738=CARTESIAN_POINT('Ctrl Pts',(19.6847718454635,17.3194985677729,4.44964764225537));
#183739=CARTESIAN_POINT('Ctrl Pts',(19.6914385166342,17.3228643425514,4.44919022194102));
#183740=CARTESIAN_POINT('Ctrl Pts',(19.7017906431506,17.3281597056926,4.44848137483088));
#183741=CARTESIAN_POINT('Ctrl Pts',(19.7054883812649,17.3300649589653,4.44822846586572));
#183742=CARTESIAN_POINT('Ctrl Pts',(19.7123454784386,17.3336236818843,4.44776004112421));
#183743=CARTESIAN_POINT('Ctrl Pts',(19.7155062457025,17.335274219155,4.44754435143771));
#183744=CARTESIAN_POINT('Ctrl Pts',(19.7226552535959,17.339030414641,4.44705701340235));
#183745=CARTESIAN_POINT('Ctrl Pts',(19.7266409346933,17.3411408302741,4.44678567017114));
#183746=CARTESIAN_POINT('Ctrl Pts',(19.7386829809241,17.3475664400183,4.44596683792301));
#183747=CARTESIAN_POINT('Ctrl Pts',(19.7467182970182,17.3519211468294,4.44542179232326));
#183748=CARTESIAN_POINT('Ctrl Pts',(19.8089338868011,17.3861617147272,4.44121009058585));
#183749=CARTESIAN_POINT('Ctrl Pts',(19.8618139611038,17.4183609351148,4.43768016365321));
#183750=CARTESIAN_POINT('Ctrl Pts',(20.0480478728177,17.5432690828335,4.42515321751982));
#183751=CARTESIAN_POINT('Ctrl Pts',(20.172036699504,17.6489167148348,4.41658701722823));
#183752=CARTESIAN_POINT('Ctrl Pts',(20.3221663732146,17.810014105773,4.40436897578582));
#183753=CARTESIAN_POINT('Ctrl Pts',(20.3598434748568,17.8539199835302,4.40111432068953));
#183754=CARTESIAN_POINT('Ctrl Pts',(20.4176865683165,17.927196780438,4.39574900570804));
#183755=CARTESIAN_POINT('Ctrl Pts',(20.4389925446789,17.9556309817743,4.39368233019728));
#183756=CARTESIAN_POINT('Ctrl Pts',(20.4659137578264,17.9935093158942,4.39094223313347));
#183757=CARTESIAN_POINT('Ctrl Pts',(20.4721859738856,18.0024809294799,4.39029417112524));
#183758=CARTESIAN_POINT('Ctrl Pts',(20.4823139372084,18.0172096579666,4.38923158516815));
#183759=CARTESIAN_POINT('Ctrl Pts',(20.4862115481139,18.0229378414109,4.38881865966345));
#183760=CARTESIAN_POINT('Ctrl Pts',(20.4936804701436,18.0340313584589,4.38801954543776));
#183761=CARTESIAN_POINT('Ctrl Pts',(20.4972555405954,18.0393940776393,4.3876335047431));
#183762=CARTESIAN_POINT('Ctrl Pts',(20.505423717685,18.0517686706659,4.38674325918683));
#183763=CARTESIAN_POINT('Ctrl Pts',(20.5099997566758,18.0587916318574,4.38623842187732));
#183764=CARTESIAN_POINT('Ctrl Pts',(20.5221290586714,18.077650710054,4.38488374041003));
#183765=CARTESIAN_POINT('Ctrl Pts',(20.5296063806551,18.0895349518028,4.38403109688649));
#183766=CARTESIAN_POINT('Ctrl Pts',(20.5910212853854,18.1893350058202,4.37687823262409));
#183767=CARTESIAN_POINT('Ctrl Pts',(20.638577948641,18.2809974257249,4.37034549701392));
#183768=CARTESIAN_POINT('Ctrl Pts',(20.7316506892097,18.4977595110238,4.35502184278328));
#183769=CARTESIAN_POINT('Ctrl Pts',(20.7724409863092,18.6244203378445,4.3461467261345));
#183770=CARTESIAN_POINT('Ctrl Pts',(20.8119977476574,18.803367633546,4.33417612650166));
#183771=CARTESIAN_POINT('Ctrl Pts',(20.8211299772893,18.8530503887307,4.33091401355052));
#183772=CARTESIAN_POINT('Ctrl Pts',(20.8323766311793,18.9295342342943,4.32602948191945));
#183773=CARTESIAN_POINT('Ctrl Pts',(20.8357723597768,18.9561263708105,4.32435641887075));
#183774=CARTESIAN_POINT('Ctrl Pts',(20.8393960422988,18.9895438402612,4.32229140049602));
#183775=CARTESIAN_POINT('Ctrl Pts',(20.8400971679454,18.9963140719649,4.32187495998678));
#183776=CARTESIAN_POINT('Ctrl Pts',(20.841159838324,19.007082059948,4.32121579789918));
#183777=CARTESIAN_POINT('Ctrl Pts',(20.8415426791791,19.0110775986074,4.32097190695017));
#183778=CARTESIAN_POINT('Ctrl Pts',(20.8422464399204,19.0186491769008,4.32051108075974));
#183779=CARTESIAN_POINT('Ctrl Pts',(20.8425696222616,19.0222248988379,4.32029402647977));
#183780=CARTESIAN_POINT('Ctrl Pts',(20.8432916071484,19.0304462515227,4.31979626683849));
#183781=CARTESIAN_POINT('Ctrl Pts',(20.8436841594525,19.0350923867969,4.31951591494739));
#183782=CARTESIAN_POINT('Ctrl Pts',(20.8446931466348,19.0475239106681,4.31876822860451));
#183783=CARTESIAN_POINT('Ctrl Pts',(20.8452818630818,19.0553115614127,4.31830240627529));
#183784=CARTESIAN_POINT('Ctrl Pts',(20.8493029369268,19.1127284213935,4.31488568765646));
#183785=CARTESIAN_POINT('Ctrl Pts',(20.8510283644945,19.1624658313344,4.31202326432112));
#183786=CARTESIAN_POINT('Ctrl Pts',(20.8509850454862,19.2375215172516,4.3077892818664));
#183787=CARTESIAN_POINT('Ctrl Pts',(20.8505169199288,19.2628196153999,4.30637685608441));
#183788=CARTESIAN_POINT('Ctrl Pts',(20.847966376092,19.3328020407431,4.30249608983154));
#183789=CARTESIAN_POINT('Ctrl Pts',(20.8449211244965,19.3774385824156,4.30005056331034));
#183790=CARTESIAN_POINT('Ctrl Pts',(20.8295689236847,19.5307423897801,4.29166236447816));
#183791=CARTESIAN_POINT('Ctrl Pts',(20.8102614474233,19.6385299134605,4.28577473614214));
#183792=CARTESIAN_POINT('Ctrl Pts',(20.7636491584859,19.8175816022643,4.27548688946047));
#183793=CARTESIAN_POINT('Ctrl Pts',(20.7406700897837,19.8897417442096,4.27119660343082));
#183794=CARTESIAN_POINT('Ctrl Pts',(20.7071894594262,19.978182741616,4.26567548336885));
#183795=CARTESIAN_POINT('Ctrl Pts',(20.7002638680072,19.9957626194925,4.26456481947438));
#183796=CARTESIAN_POINT('Ctrl Pts',(20.689856297566,20.0211781245116,4.26293887504148));
#183797=CARTESIAN_POINT('Ctrl Pts',(20.6865604452736,20.0290893315671,4.26242988068077));
#183798=CARTESIAN_POINT('Ctrl Pts',(20.6806994275023,20.0429206477881,4.26153484715167));
#183799=CARTESIAN_POINT('Ctrl Pts',(20.678155051288,20.0488494855182,4.26114951923809));
#183800=CARTESIAN_POINT('Ctrl Pts',(20.6731631215181,20.0603363703092,4.26039967737386));
#183801=CARTESIAN_POINT('Ctrl Pts',(20.6707186724163,20.0658957038753,4.26003527259443));
#183802=CARTESIAN_POINT('Ctrl Pts',(20.6648199476168,20.0791558408141,4.25916246134555));
#183803=CARTESIAN_POINT('Ctrl Pts',(20.6613434940297,20.0868466114845,4.25865329663248));
#183804=CARTESIAN_POINT('Ctrl Pts',(20.6486451341995,20.1144967788622,4.25681196863498));
#183805=CARTESIAN_POINT('Ctrl Pts',(20.6391586573169,20.1343324713022,4.25547070827276));
#183806=CARTESIAN_POINT('Ctrl Pts',(20.5461444221216,20.321281475077,4.24263087342255));
#183807=CARTESIAN_POINT('Ctrl Pts',(20.4411625535529,20.4767646797961,4.23032076965095));
#183808=CARTESIAN_POINT('Ctrl Pts',(20.2645101541816,20.6757604232352,4.2127549692487));
#183809=CARTESIAN_POINT('Ctrl Pts',(20.2085379075336,20.7320930542604,4.20754382136202));
#183810=CARTESIAN_POINT('Ctrl Pts',(20.1229024828073,20.8090993150867,4.2002037819797));
#183811=CARTESIAN_POINT('Ctrl Pts',(20.0956679702627,20.8323673916213,4.19795411955092));
#183812=CARTESIAN_POINT('Ctrl Pts',(20.0620668102219,20.8596306728855,4.19529210312768));
#183813=CARTESIAN_POINT('Ctrl Pts',(20.0562543606948,20.8642960888521,4.19483560586379));
#183814=CARTESIAN_POINT('Ctrl Pts',(20.0471621908427,20.8715153827546,4.19412787514434));
#183815=CARTESIAN_POINT('Ctrl Pts',(20.0438994494595,20.8740904090923,4.19387516690331));
#183816=CARTESIAN_POINT('Ctrl Pts',(20.0378232721616,20.8788568860486,4.193406924065));
#183817=CARTESIAN_POINT('Ctrl Pts',(20.0350119097749,20.8810508160734,4.19319121674709));
#183818=CARTESIAN_POINT('Ctrl Pts',(20.0286290682728,20.886005956539,4.19270359746959));
#183819=CARTESIAN_POINT('Ctrl Pts',(20.0250543020063,20.8887628464704,4.19243199211841));
#183820=CARTESIAN_POINT('Ctrl Pts',(20.0144334222189,20.8968997128722,4.19162934855027));
#183821=CARTESIAN_POINT('Ctrl Pts',(20.007362202665,20.9022469652986,4.19110056120902));
#183822=CARTESIAN_POINT('Ctrl Pts',(19.9544652561465,20.9417277724259,4.18718469241085));
#183823=CARTESIAN_POINT('Ctrl Pts',(19.9073036182297,20.9740410972697,4.18391410124965));
#183824=CARTESIAN_POINT('Ctrl Pts',(19.7306439796643,21.084848107821,4.17222252573817));
#183825=CARTESIAN_POINT('Ctrl Pts',(19.5941366166486,21.1513032000611,4.16420726557329));
#183826=CARTESIAN_POINT('Ctrl Pts',(19.3644837038337,21.2340605367309,4.15076198119429));
#183827=CARTESIAN_POINT('Ctrl Pts',(19.2753056437404,21.25972373936,4.14555620143176));
#183828=CARTESIAN_POINT('Ctrl Pts',(19.1641535764797,21.2839449564784,4.13892973150984));
#183829=CARTESIAN_POINT('Ctrl Pts',(19.1435026764916,21.2881231072552,4.13769319852282));
#183830=CARTESIAN_POINT('Ctrl Pts',(19.1139907029175,21.2936368521036,4.13591708175391));
#183831=CARTESIAN_POINT('Ctrl Pts',(19.1051777748455,21.2952255750641,4.13538555869002));
#183832=CARTESIAN_POINT('Ctrl Pts',(19.089934784856,21.2978737129783,4.13446416541299));
#183833=CARTESIAN_POINT('Ctrl Pts',(19.0835093761036,21.2989594487302,4.13407513744572));
#183834=CARTESIAN_POINT('Ctrl Pts',(19.0711817060508,21.3009840225588,4.13332750714668));
#183835=CARTESIAN_POINT('Ctrl Pts',(19.0652802731353,21.3019275685541,4.13296905845384));
#183836=CARTESIAN_POINT('Ctrl Pts',(19.0498903480064,21.3043213853953,4.13203282292778));
#183837=CARTESIAN_POINT('Ctrl Pts',(19.0403959264125,21.3057321227421,4.13145378884814));
#183838=CARTESIAN_POINT('Ctrl Pts',(19.007813275751,21.3103471890729,4.12946154353478));
#183839=CARTESIAN_POINT('Ctrl Pts',(18.9846825382579,21.3132346508188,4.12803838230219));
#183840=CARTESIAN_POINT('Ctrl Pts',(18.7917169114187,21.3340930616151,4.11608809622742));
#183841=CARTESIAN_POINT('Ctrl Pts',(18.6203576101351,21.3318298199412,4.10489913059937));
#183842=CARTESIAN_POINT('Ctrl Pts',(18.3616269040043,21.2969508424641,4.08764705330503));
#183843=CARTESIAN_POINT('Ctrl Pts',(18.2729430385332,21.2791588707252,4.08168387113909));
#183844=CARTESIAN_POINT('Ctrl Pts',(18.1483262681061,21.2457406615571,4.07344069716556));
#183845=CARTESIAN_POINT('Ctrl Pts',(18.1112679907923,21.2347066389032,4.07100779510073));
#183846=CARTESIAN_POINT('Ctrl Pts',(18.0672905625408,21.2202898173554,4.06815963130051));
#183847=CARTESIAN_POINT('Ctrl Pts',(18.0600637171953,21.2178774090351,4.06769286947869));
#183848=CARTESIAN_POINT('Ctrl Pts',(18.0488804371117,21.2140770731554,4.06697273236148));
#183849=CARTESIAN_POINT('Ctrl Pts',(18.0449149223821,21.2127163467786,4.06671779928892));
#183850=CARTESIAN_POINT('Ctrl Pts',(18.0375868579237,21.2101774383176,4.06624751356651));
#183851=CARTESIAN_POINT('Ctrl Pts',(18.0342232680884,21.2090025575856,4.06603197507602));
#183852=CARTESIAN_POINT('Ctrl Pts',(18.0266492763542,21.2063355374058,4.06554735206495));
#183853=CARTESIAN_POINT('Ctrl Pts',(18.0224406340152,21.2048385648285,4.06527855813702));
#183854=CARTESIAN_POINT('Ctrl Pts',(18.0101012265045,21.2004055128176,4.06449184810243));
#183855=CARTESIAN_POINT('Ctrl Pts',(18.0019835573429,21.1974328989824,4.06397605202905));
#183856=CARTESIAN_POINT('Ctrl Pts',(17.9455380684285,21.1763700891682,4.06040025890264));
#183857=CARTESIAN_POINT('Ctrl Pts',(17.8978634089018,21.1565663282831,4.05743505752371));
#183858=CARTESIAN_POINT('Ctrl Pts',(17.8310742971141,21.1259132445387,4.05329618696102));
#183859=CARTESIAN_POINT('Ctrl Pts',(17.8113344211655,21.1164804733937,4.05207488749926));
#183860=CARTESIAN_POINT('Ctrl Pts',(17.6684448828543,21.045458962789,4.04322466702742));
#183861=CARTESIAN_POINT('Ctrl Pts',(17.551416570879,20.9722911392629,4.03590130831542));
#183862=CARTESIAN_POINT('Ctrl Pts',(17.3704325365416,20.8329140651624,4.02330709170845));
#183863=CARTESIAN_POINT('Ctrl Pts',(17.3021867902169,20.7729954100742,4.01820659106598));
#183864=CARTESIAN_POINT('Ctrl Pts',(17.2232621122057,20.6941702018384,4.0117074889394));
#183865=CARTESIAN_POINT('Ctrl Pts',(17.2087434996877,20.6792354633583,4.01048486823811));
#183866=CARTESIAN_POINT('Ctrl Pts',(17.1883296402444,20.6576069246604,4.00872528437738));
#183867=CARTESIAN_POINT('Ctrl Pts',(17.1822523782327,20.6510860287288,4.00819617505904));
#183868=CARTESIAN_POINT('Ctrl Pts',(17.1718088669142,20.6397372861871,4.00727763160153));
#183869=CARTESIAN_POINT('Ctrl Pts',(17.1674233367316,20.6349272895329,4.0068890254886));
#183870=CARTESIAN_POINT('Ctrl Pts',(17.1590478571406,20.6256556376418,4.00614126433629));
#183871=CARTESIAN_POINT('Ctrl Pts',(17.1550545045477,20.6211971304241,4.00578225841507));
#183872=CARTESIAN_POINT('Ctrl Pts',(17.144673732083,20.6095078110725,4.00484247169327));
#183873=CARTESIAN_POINT('Ctrl Pts',(17.1383167941504,20.6022502238171,4.00426042502176));
#183874=CARTESIAN_POINT('Ctrl Pts',(17.1165780819839,20.5770865861418,4.00224710074462));
#183875=CARTESIAN_POINT('Ctrl Pts',(17.1014467602915,20.5589673847883,4.00080558837357));
#183876=CARTESIAN_POINT('Ctrl Pts',(16.9829322115398,20.4121274881097,3.98918378689565));
#183877=CARTESIAN_POINT('Ctrl Pts',(16.8946452062152,20.2719900612155,3.9783899723475));
#183878=CARTESIAN_POINT('Ctrl Pts',(16.7945495531224,20.0623225585219,3.96303632113798));
#183879=CARTESIAN_POINT('Ctrl Pts',(16.7684811856473,20.0002690983787,3.95859027556942));
#183880=CARTESIAN_POINT('Ctrl Pts',(16.7454192928009,19.9371100267559,3.95421654644109));
#183881=CARTESIAN_POINT('',(16.6170007560323,19.2092108548856,4.48828854928401));
#183882=CARTESIAN_POINT('Ctrl Pts',(16.7454193623262,19.9371102171632,3.73234496441554));
#183883=CARTESIAN_POINT('Ctrl Pts',(16.7511301821152,19.9527503023585,3.73327488216032));
#183884=CARTESIAN_POINT('Ctrl Pts',(16.7570271402811,19.9683274681955,3.73420935652883));
#183885=CARTESIAN_POINT('Ctrl Pts',(16.7847361246994,20.0389908547596,3.73849007279982));
#183886=CARTESIAN_POINT('Ctrl Pts',(16.8086666919897,20.09320702465,3.74189144616012));
#183887=CARTESIAN_POINT('Ctrl Pts',(16.8402460982925,20.1573271180286,3.74609042516054));
#183888=CARTESIAN_POINT('Ctrl Pts',(16.8457497773428,20.1682616892724,3.74681280859572));
#183889=CARTESIAN_POINT('Ctrl Pts',(16.8549744682823,20.1861999470631,3.74800862032513));
#183890=CARTESIAN_POINT('Ctrl Pts',(16.8586405989902,20.1932316427534,3.74848011759585));
#183891=CARTESIAN_POINT('Ctrl Pts',(16.8653238737509,20.2058764463867,3.74933303018163));
#183892=CARTESIAN_POINT('Ctrl Pts',(16.868327032131,20.2114968685499,3.74971394621964));
#183893=CARTESIAN_POINT('Ctrl Pts',(16.8748001947079,20.2234809233867,3.7505300649941));
#183894=CARTESIAN_POINT('Ctrl Pts',(16.8782775889256,20.2298404522894,3.75096552794722));
#183895=CARTESIAN_POINT('Ctrl Pts',(16.8877881929084,20.2470234112969,3.75214863950455));
#183896=CARTESIAN_POINT('Ctrl Pts',(16.8938838139386,20.2578118058947,3.75289851996892));
#183897=CARTESIAN_POINT('Ctrl Pts',(16.9256758973077,20.3129435392721,3.75676757530466));
#183898=CARTESIAN_POINT('Ctrl Pts',(16.9528799516673,20.3563935066497,3.75994114839642));
#183899=CARTESIAN_POINT('Ctrl Pts',(17.0774339827088,20.5401470878826,3.77392296576256));
#183900=CARTESIAN_POINT('Ctrl Pts',(17.1899739660393,20.6693586488334,3.78529469876379));
#183901=CARTESIAN_POINT('Ctrl Pts',(17.3851491458625,20.8452464628246,3.80257303113745));
#183902=CARTESIAN_POINT('Ctrl Pts',(17.4574748771101,20.9023449443682,3.80854929797737));
#183903=CARTESIAN_POINT('Ctrl Pts',(17.5412586065262,20.9600427229839,3.81483427810208));
#183904=CARTESIAN_POINT('Ctrl Pts',(17.5492591626678,20.9654718963341,3.8154283180293));
#183905=CARTESIAN_POINT('Ctrl Pts',(17.5611326750265,20.973410999223,3.81630059436935));
#183906=CARTESIAN_POINT('Ctrl Pts',(17.5649769621597,20.9759632942649,3.81658157941001));
#183907=CARTESIAN_POINT('Ctrl Pts',(17.5718145081591,20.9804707299225,3.81707876634139));
#183908=CARTESIAN_POINT('Ctrl Pts',(17.5748044019134,20.9824308757475,3.81729530137233));
#183909=CARTESIAN_POINT('Ctrl Pts',(17.5812240084211,20.9866162950421,3.81775834667016));
#183910=CARTESIAN_POINT('Ctrl Pts',(17.5846551961659,20.9888392043517,3.81800469954061));
#183911=CARTESIAN_POINT('Ctrl Pts',(17.5940984741114,20.9949183069583,3.81867965074302));
#183912=CARTESIAN_POINT('Ctrl Pts',(17.600123737696,20.9987540769686,3.81910691013807));
#183913=CARTESIAN_POINT('Ctrl Pts',(17.6325052762639,21.0191390688196,3.82138566464375));
#183914=CARTESIAN_POINT('Ctrl Pts',(17.6592061385684,21.0351370302697,3.82320298173722));
#183915=CARTESIAN_POINT('Ctrl Pts',(17.8286691088471,21.1316581314889,3.83441819100461));
#183916=CARTESIAN_POINT('Ctrl Pts',(17.9800399028227,21.1959705874623,3.84307890089296));
#183917=CARTESIAN_POINT('Ctrl Pts',(18.2497877737525,21.2752106474579,3.85846828558921));
#183918=CARTESIAN_POINT('Ctrl Pts',(18.364779672467,21.2988453318533,3.86501034735576));
#183919=CARTESIAN_POINT('Ctrl Pts',(18.4953201014908,21.314550628943,3.87271294160433));
#183920=CARTESIAN_POINT('Ctrl Pts',(18.5095292597716,21.3161142995894,3.87355473649914));
#183921=CARTESIAN_POINT('Ctrl Pts',(18.532167243713,21.318373731634,3.8749016897327));
#183922=CARTESIAN_POINT('Ctrl Pts',(18.540586438649,21.3191631097741,3.87540390428919));
#183923=CARTESIAN_POINT('Ctrl Pts',(18.555442409567,21.3204662549038,3.87629241448077));
#183924=CARTESIAN_POINT('Ctrl Pts',(18.5618772661775,21.3210010561028,3.87667804361802));
#183925=CARTESIAN_POINT('Ctrl Pts',(18.575190856235,21.3220462412589,3.87747753837022));
#183926=CARTESIAN_POINT('Ctrl Pts',(18.5820698311541,21.3225524617967,3.87789153010235));
#183927=CARTESIAN_POINT('Ctrl Pts',(18.599731997879,21.3237654578034,3.87895684845167));
#183928=CARTESIAN_POINT('Ctrl Pts',(18.6105182519822,21.3244232957944,3.87960970350795));
#183929=CARTESIAN_POINT('Ctrl Pts',(18.6555452821222,21.326823555215,3.88234478651855));
#183930=CARTESIAN_POINT('Ctrl Pts',(18.6898192381527,21.3278165494257,3.88445032496534));
#183931=CARTESIAN_POINT('Ctrl Pts',(18.7791605186645,21.3282343230201,3.89000354071703));
#183932=CARTESIAN_POINT('Ctrl Pts',(18.8342053197233,21.3263436425017,3.89348958172809));
#183933=CARTESIAN_POINT('Ctrl Pts',(18.9981747699146,21.3142973973527,3.90405711093055));
#183934=CARTESIAN_POINT('Ctrl Pts',(19.1064469642927,21.297846434864,3.91128699662245));
#183935=CARTESIAN_POINT('Ctrl Pts',(19.2565082286312,21.2629925501149,3.92146357903006));
#183936=CARTESIAN_POINT('Ctrl Pts',(19.299731676814,21.251498988194,3.92441190518347));
#183937=CARTESIAN_POINT('Ctrl Pts',(19.3667225416407,21.2313929390796,3.92898244881481));
#183938=CARTESIAN_POINT('Ctrl Pts',(19.3907546696953,21.2237093227024,3.93062221528891));
#183939=CARTESIAN_POINT('Ctrl Pts',(19.4618699183207,21.1995627370261,3.9354647701689));
#183940=CARTESIAN_POINT('Ctrl Pts',(19.5085183824853,21.1818623794304,3.93862853329498));
#183941=CARTESIAN_POINT('Ctrl Pts',(19.5617057662208,21.1595002531938,3.94218669749329));
#183942=CARTESIAN_POINT('Ctrl Pts',(19.5688931004567,21.1564314655755,3.94266645739698));
#183943=CARTESIAN_POINT('Ctrl Pts',(19.5803426983136,21.1514676733282,3.94342883303313));
#183944=CARTESIAN_POINT('Ctrl Pts',(19.5846158989509,21.14959829455,3.94371294225333));
#183945=CARTESIAN_POINT('Ctrl Pts',(19.5921676628061,21.1462648795954,3.94421423489702));
#183946=CARTESIAN_POINT('Ctrl Pts',(19.5954487225084,21.1448066063882,3.94443176603009));
#183947=CARTESIAN_POINT('Ctrl Pts',(19.6023890420888,21.141700799033,3.94489131938518));
#183948=CARTESIAN_POINT('Ctrl Pts',(19.6060473249025,21.1400512091579,3.94513321315618));
#183949=CARTESIAN_POINT('Ctrl Pts',(19.6158941963951,21.1355773304388,3.94578345193418));
#183950=CARTESIAN_POINT('Ctrl Pts',(19.6220739601781,21.1327335711796,3.94619061688297));
#183951=CARTESIAN_POINT('Ctrl Pts',(19.6524951793011,21.1185564708656,3.94819096060612));
#183952=CARTESIAN_POINT('Ctrl Pts',(19.6765351380951,21.1067934350036,3.94975909388299));
#183953=CARTESIAN_POINT('Ctrl Pts',(19.745164350161,21.0715840345379,3.95421742031739));
#183954=CARTESIAN_POINT('Ctrl Pts',(19.7891500424924,21.0469971016158,3.957052200249));
#183955=CARTESIAN_POINT('Ctrl Pts',(19.9451763115874,20.9523208244569,3.96717294494502));
#183956=CARTESIAN_POINT('Ctrl Pts',(20.051470904392,20.8733534911066,3.97421147531152));
#183957=CARTESIAN_POINT('Ctrl Pts',(20.2269856781593,20.7154880447386,3.98719791917516));
#183958=CARTESIAN_POINT('Ctrl Pts',(20.2990255553218,20.6403989932548,3.993036777261));
#183959=CARTESIAN_POINT('Ctrl Pts',(20.3742161634738,20.5494982460048,3.99994988372352));
#183960=CARTESIAN_POINT('Ctrl Pts',(20.3830679244672,20.538577336266,4.00077790081263));
#183961=CARTESIAN_POINT('Ctrl Pts',(20.3970261306588,20.521001310588,4.0021069158685));
#183962=CARTESIAN_POINT('Ctrl Pts',(20.4022030170933,20.5144024841423,4.00260509286901));
#183963=CARTESIAN_POINT('Ctrl Pts',(20.4112889757448,20.5026780721383,4.0034889114461));
#183964=CARTESIAN_POINT('Ctrl Pts',(20.4152141281474,20.4975650407565,4.00387390911743));
#183965=CARTESIAN_POINT('Ctrl Pts',(20.4233084062267,20.4869208765084,4.00467452443063));
#183966=CARTESIAN_POINT('Ctrl Pts',(20.4274738556524,20.481387056336,4.00509028019656));
#183967=CARTESIAN_POINT('Ctrl Pts',(20.4381465718692,20.4670625310526,4.006165309773));
#183968=CARTESIAN_POINT('Ctrl Pts',(20.4446129458923,20.4582417418618,4.00682616614534));
#183969=CARTESIAN_POINT('Ctrl Pts',(20.4717422470376,20.4206267756346,4.00963984808525));
#183970=CARTESIAN_POINT('Ctrl Pts',(20.4917477587546,20.391367583306,4.01181769228642));
#183971=CARTESIAN_POINT('Ctrl Pts',(20.5423374306959,20.3132373819067,4.01760876797445));
#183972=CARTESIAN_POINT('Ctrl Pts',(20.5716747307795,20.263597815947,4.02126458655133));
#183973=CARTESIAN_POINT('Ctrl Pts',(20.6748472495638,20.0715371932385,4.03530635020058));
#183974=CARTESIAN_POINT('Ctrl Pts',(20.734436356534,19.9220972779059,4.04607404844624));
#183975=CARTESIAN_POINT('Ctrl Pts',(20.7803420205634,19.7535662092129,4.05743444086405));
#183976=CARTESIAN_POINT('Ctrl Pts',(20.7839626653809,19.7397218938321,4.05836171553017));
#183977=CARTESIAN_POINT('Ctrl Pts',(20.7900540294908,19.7154265284647,4.05997749123066));
#183978=CARTESIAN_POINT('Ctrl Pts',(20.7925860980395,19.7049914764026,4.06066779031244));
#183979=CARTESIAN_POINT('Ctrl Pts',(20.804329950576,19.6549342693205,4.0639601981538));
#183980=CARTESIAN_POINT('Ctrl Pts',(20.8124785173306,19.6150684232819,4.06652563870022));
#183981=CARTESIAN_POINT('Ctrl Pts',(20.8207403122214,19.5677325877238,4.0694861224246));
#183982=CARTESIAN_POINT('Ctrl Pts',(20.8219690674966,19.56046880634,4.06993804565851));
#183983=CARTESIAN_POINT('Ctrl Pts',(20.82390032049,19.5486782967923,4.07066760133132));
#183984=CARTESIAN_POINT('Ctrl Pts',(20.8246260750177,19.5441555148515,4.07094650206992));
#183985=CARTESIAN_POINT('Ctrl Pts',(20.8258916127203,19.5361018889429,4.07144139573215));
#183986=CARTESIAN_POINT('Ctrl Pts',(20.8264371442872,19.5325720065961,4.07165771024461));
#183987=CARTESIAN_POINT('Ctrl Pts',(20.8275912306148,19.5249771530222,4.07212184025405));
#183988=CARTESIAN_POINT('Ctrl Pts',(20.8281968799802,19.5209117972402,4.07236949017658));
#183989=CARTESIAN_POINT('Ctrl Pts',(20.8298369351921,19.5096787341877,4.07305166327479));
#183990=CARTESIAN_POINT('Ctrl Pts',(20.8308464188975,19.5025073655581,4.07348479944763));
#183991=CARTESIAN_POINT('Ctrl Pts',(20.8361896723677,19.463084349893,4.07585353081452));
#183992=CARTESIAN_POINT('Ctrl Pts',(20.8398164250681,19.4307393548967,4.07775167274199));
#183993=CARTESIAN_POINT('Ctrl Pts',(20.8570905572145,19.2362829465584,4.08896056158089));
#183994=CARTESIAN_POINT('Ctrl Pts',(20.8527615479326,19.0731084315824,4.09755904451648));
#183995=CARTESIAN_POINT('Ctrl Pts',(20.8132821694725,18.796361307802,4.11286292887981));
#183996=CARTESIAN_POINT('Ctrl Pts',(20.7872378520925,18.6822763982243,4.1193853311666));
#183997=CARTESIAN_POINT('Ctrl Pts',(20.7475991240023,18.5573091158752,4.12706579577597));
#183998=CARTESIAN_POINT('Ctrl Pts',(20.7431408526149,18.5437322699136,4.12790730965704));
#183999=CARTESIAN_POINT('Ctrl Pts',(20.735826624203,18.5221962186447,4.12925389722875));
#184000=CARTESIAN_POINT('Ctrl Pts',(20.733059793352,18.5142070450861,4.12975602966671));
#184001=CARTESIAN_POINT('Ctrl Pts',(20.7280956811924,18.5001462140787,4.13064444419981));
#184002=CARTESIAN_POINT('Ctrl Pts',(20.7259183273438,18.494067599787,4.13103006025751));
#184003=CARTESIAN_POINT('Ctrl Pts',(20.7213573450474,18.4815156836372,4.1318295766242));
#184004=CARTESIAN_POINT('Ctrl Pts',(20.718969819617,18.4750438884075,4.13224360329056));
#184005=CARTESIAN_POINT('Ctrl Pts',(20.712760130278,18.4584615099707,4.13330911417358));
#184006=CARTESIAN_POINT('Ctrl Pts',(20.708892120634,18.4483684131737,4.13396212789599));
#184007=CARTESIAN_POINT('Ctrl Pts',(20.6924249575182,18.4063648691136,4.13669874835442));
#184008=CARTESIAN_POINT('Ctrl Pts',(20.6791289124934,18.3747349071465,4.13880569837287));
#184009=CARTESIAN_POINT('Ctrl Pts',(20.6424863319229,18.2931731811083,4.14436352470528));
#184010=CARTESIAN_POINT('Ctrl Pts',(20.6179492061051,18.2438078183229,4.14785284419523));
#184011=CARTESIAN_POINT('Ctrl Pts',(20.539036006608,18.099468472681,4.15842667129756));
#184012=CARTESIAN_POINT('Ctrl Pts',(20.4791978374525,18.0076968944616,4.16565955547208));
#184013=CARTESIAN_POINT('Ctrl Pts',(20.3829258539305,17.8824313188052,4.17609570544941));
#184014=CARTESIAN_POINT('Ctrl Pts',(20.3519898988495,17.8449252803927,4.17929988068426));
#184015=CARTESIAN_POINT('Ctrl Pts',(20.3082127701791,17.7954264309714,4.18361043941861));
#184016=CARTESIAN_POINT('Ctrl Pts',(20.2964739656836,17.7824799597491,4.18474583892938));
#184017=CARTESIAN_POINT('Ctrl Pts',(20.248242296192,17.7305921952975,4.18932440718615));
#184018=CARTESIAN_POINT('Ctrl Pts',(20.2104400998258,17.6928884530024,4.19271695928357));
#184019=CARTESIAN_POINT('Ctrl Pts',(20.1648465366104,17.650729750702,4.19654762693061));
#184020=CARTESIAN_POINT('Ctrl Pts',(20.1584064595039,17.6448482492715,4.19708291812731));
#184021=CARTESIAN_POINT('Ctrl Pts',(20.1486008733891,17.6360036602078,4.19788897655025));
#184022=CARTESIAN_POINT('Ctrl Pts',(20.1452620866617,17.6330112722332,4.19816188140133));
#184023=CARTESIAN_POINT('Ctrl Pts',(20.1392522501189,17.6276592864699,4.19865028426725));
#184024=CARTESIAN_POINT('Ctrl Pts',(20.1365847376583,17.6252958170394,4.19886607051818));
#184025=CARTESIAN_POINT('Ctrl Pts',(20.130775933192,17.620175226162,4.19933380738383));
#184026=CARTESIAN_POINT('Ctrl Pts',(20.1276324510737,17.617420676399,4.19958556707161));
#184027=CARTESIAN_POINT('Ctrl Pts',(20.1187807147261,17.6097103588029,4.200290755988));
#184028=CARTESIAN_POINT('Ctrl Pts',(20.1130539785424,17.6047757718627,4.20074263999201));
#184029=CARTESIAN_POINT('Ctrl Pts',(20.078681222448,17.575476963071,4.20342992675701));
#184030=CARTESIAN_POINT('Ctrl Pts',(20.0494146553293,17.5518472427578,4.20561499482981));
#184031=CARTESIAN_POINT('Ctrl Pts',(19.9510800007609,17.4766908967316,4.21268292987606));
#184032=CARTESIAN_POINT('Ctrl Pts',(19.8794923075859,17.4285967028176,4.21740284219613));
#184033=CARTESIAN_POINT('Ctrl Pts',(19.652760223261,17.2955914476036,4.23170833242908));
#184034=CARTESIAN_POINT('Ctrl Pts',(19.4897789349949,17.225628037314,4.24120189414262));
#184035=CARTESIAN_POINT('Ctrl Pts',(19.2979991984338,17.1703828406183,4.25280013293854));
#184036=CARTESIAN_POINT('Ctrl Pts',(19.275891651757,17.1644011471386,4.25414192076161));
#184037=CARTESIAN_POINT('Ctrl Pts',(19.2444522316823,17.1564396168952,4.25605858487251));
#184038=CARTESIAN_POINT('Ctrl Pts',(19.2351968555555,17.1541622436083,4.25662385775803));
#184039=CARTESIAN_POINT('Ctrl Pts',(19.2201255907791,17.1505615802483,4.25754612771147));
#184040=CARTESIAN_POINT('Ctrl Pts',(19.2143188677942,17.1492002144439,4.25790189445531));
#184041=CARTESIAN_POINT('Ctrl Pts',(19.202145593783,17.1464004493345,4.25864866184819));
#184042=CARTESIAN_POINT('Ctrl Pts',(19.1957779970397,17.1449669214759,4.25903981477013));
#184043=CARTESIAN_POINT('Ctrl Pts',(19.1806020097951,17.1416240366475,4.25997337020758));
#184044=CARTESIAN_POINT('Ctrl Pts',(19.1717879087025,17.1397414512135,4.26051662463915));
#184045=CARTESIAN_POINT('Ctrl Pts',(19.1419962260148,17.1335769640033,4.26235652089195));
#184046=CARTESIAN_POINT('Ctrl Pts',(19.1209663205808,17.1295571339028,4.2636614863055));
#184047=CARTESIAN_POINT('Ctrl Pts',(19.0707591494819,17.1207472907047,4.26679266250234));
#184048=CARTESIAN_POINT('Ctrl Pts',(19.0415360081633,17.1162483247721,4.26862772596779));
#184049=CARTESIAN_POINT('Ctrl Pts',(18.8433399762533,17.0899722470197,4.28116047324447));
#184050=CARTESIAN_POINT('Ctrl Pts',(18.6723859150249,17.0880539624159,4.29247013483993));
#184051=CARTESIAN_POINT('Ctrl Pts',(18.4039177274325,17.1175130311433,4.31026446637037));
#184052=CARTESIAN_POINT('Ctrl Pts',(18.3056290285557,17.1353928516231,4.31676737978444));
#184053=CARTESIAN_POINT('Ctrl Pts',(18.1995669030097,17.1625458891058,4.32353171879714));
#184054=CARTESIAN_POINT('Ctrl Pts',(18.1901918947276,17.1650147281953,4.32412736837289));
#184055=CARTESIAN_POINT('Ctrl Pts',(18.1763750873564,17.168754961962,4.32500154770153));
#184056=CARTESIAN_POINT('Ctrl Pts',(18.1719201139787,17.1699765946331,4.32528284306209));
#184057=CARTESIAN_POINT('Ctrl Pts',(18.1640238944989,17.1721696921031,4.32578037289907));
#184058=CARTESIAN_POINT('Ctrl Pts',(18.1605810787145,17.1731353021771,4.32599694223401));
#184059=CARTESIAN_POINT('Ctrl Pts',(18.1532101312084,17.1752227979552,4.3264598328136));
#184060=CARTESIAN_POINT('Ctrl Pts',(18.1492828063066,17.1763473288778,4.32670599785414));
#184061=CARTESIAN_POINT('Ctrl Pts',(18.1385117411464,17.1794652247564,4.32737990468372));
#184062=CARTESIAN_POINT('Ctrl Pts',(18.1316747023671,17.1814818186134,4.32780631442492));
#184063=CARTESIAN_POINT('Ctrl Pts',(18.0952340580444,17.1924304039529,4.3300724069481));
#184064=CARTESIAN_POINT('Ctrl Pts',(18.0658169643747,17.2019761572843,4.33187835986588));
#184065=CARTESIAN_POINT('Ctrl Pts',(17.9774234879568,17.2328161143402,4.33726332377545));
#184066=CARTESIAN_POINT('Ctrl Pts',(17.9191712243516,17.2560895879849,4.3407556046472));
#184067=CARTESIAN_POINT('Ctrl Pts',(17.7219704824632,17.3452263591626,4.35264921063547));
#184068=CARTESIAN_POINT('Ctrl Pts',(17.5892222465102,17.4235998150079,4.36081661934816));
#184069=CARTESIAN_POINT('Ctrl Pts',(17.4622379451329,17.5185656955367,4.36970909194733));
#184070=CARTESIAN_POINT('Ctrl Pts',(17.4583576730518,17.5214884574539,4.36998190656997));
#184071=CARTESIAN_POINT('Ctrl Pts',(17.4040559894782,17.5626841724968,4.37381531045745));
#184072=CARTESIAN_POINT('Ctrl Pts',(17.3553699636836,17.6031833921581,4.37744243492799));
#184073=CARTESIAN_POINT('Ctrl Pts',(17.2993257763103,17.6542227687575,4.38189394337219));
#184074=CARTESIAN_POINT('Ctrl Pts',(17.2901522356764,17.6627270591928,4.38263190245978));
#184075=CARTESIAN_POINT('Ctrl Pts',(17.2752274300407,17.6768110331675,4.38384822353941));
#184076=CARTESIAN_POINT('Ctrl Pts',(17.2694314413727,17.6823430302392,4.38432453714664));
#184077=CARTESIAN_POINT('Ctrl Pts',(17.2590770538952,17.6923387458035,4.38518268539031));
#184078=CARTESIAN_POINT('Ctrl Pts',(17.2545071441326,17.6967904405254,4.38556399370994));
#184079=CARTESIAN_POINT('Ctrl Pts',(17.2456932667028,17.7054543113126,4.38630444032412));
#184080=CARTESIAN_POINT('Ctrl Pts',(17.2414468806048,17.7096639490957,4.38666346498749));
#184081=CARTESIAN_POINT('Ctrl Pts',(17.2299423096576,17.7211660077224,4.38764244923022));
#184082=CARTESIAN_POINT('Ctrl Pts',(17.2227194320461,17.7284933728659,4.38826395954503));
#184083=CARTESIAN_POINT('Ctrl Pts',(17.1934249002735,17.7586482486085,4.3908132405388));
#184084=CARTESIAN_POINT('Ctrl Pts',(17.1718156648956,17.7819173645032,4.39276088741411));
#184085=CARTESIAN_POINT('Ctrl Pts',(17.1176146314886,17.8429805655847,4.39782553338901));
#184086=CARTESIAN_POINT('Ctrl Pts',(17.0858224785269,17.8814553148506,4.40097334406224));
#184087=CARTESIAN_POINT('Ctrl Pts',(17.0102401862086,17.979805947295,4.40891137003979));
#184088=CARTESIAN_POINT('Ctrl Pts',(16.9681823525145,18.0409259369875,4.4137521554419));
#184089=CARTESIAN_POINT('Ctrl Pts',(16.8493473163932,18.2346666673104,4.4287220229877));
#184090=CARTESIAN_POINT('Ctrl Pts',(16.7836721177527,18.3735217592032,4.43897492035189));
#184091=CARTESIAN_POINT('Ctrl Pts',(16.7284957692046,18.5328550914531,4.44949009444052));
#184092=CARTESIAN_POINT('Ctrl Pts',(16.7235995322683,18.5475109436552,4.45044586116425));
#184093=CARTESIAN_POINT('Ctrl Pts',(16.7171006633379,18.5676966703732,4.45174534234653));
#184094=CARTESIAN_POINT('Ctrl Pts',(16.7153596036074,18.5731810131652,4.45209670097354));
#184095=CARTESIAN_POINT('Ctrl Pts',(16.7126241714508,18.5819210329939,4.45265385356486));
#184096=CARTESIAN_POINT('Ctrl Pts',(16.7116152683634,18.5851720806839,4.45286048780106));
#184097=CARTESIAN_POINT('Ctrl Pts',(16.7095441622783,18.591903238379,4.45328703080189));
#184098=CARTESIAN_POINT('Ctrl Pts',(16.7084830888906,18.5953836567293,4.45350686751352));
#184099=CARTESIAN_POINT('Ctrl Pts',(16.7059703322528,18.603702556673,4.454030656143));
#184100=CARTESIAN_POINT('Ctrl Pts',(16.7045269724976,18.608543570224,4.45433412242644));
#184101=CARTESIAN_POINT('Ctrl Pts',(16.6996912589511,18.624977100747,4.45535988326835));
#184102=CARTESIAN_POINT('Ctrl Pts',(16.6963807210238,18.6365937138202,4.45607756803336));
#184103=CARTESIAN_POINT('Ctrl Pts',(16.6886498122196,18.6646295124094,4.45779325749149));
#184104=CARTESIAN_POINT('Ctrl Pts',(16.684327409838,18.6810750893408,4.45878621427896));
#184105=CARTESIAN_POINT('Ctrl Pts',(16.6687721137264,18.743298771819,4.46249873032591));
#184106=CARTESIAN_POINT('Ctrl Pts',(16.658870342443,18.7893981275048,4.46515906548827));
#184107=CARTESIAN_POINT('Ctrl Pts',(16.6283221861243,18.9590285268923,4.47474467553596));
#184108=CARTESIAN_POINT('Ctrl Pts',(16.6171065839527,19.0839903651149,4.48142927455064));
#184109=CARTESIAN_POINT('Ctrl Pts',(16.6170007560323,19.2092108548856,4.48828854928401));
#184110=CARTESIAN_POINT('Ctrl Pts',(16.6170007544018,19.2092127851992,4.48828865502192));
#184111=CARTESIAN_POINT('Ctrl Pts',(16.6169304738953,19.2924617484522,4.49284883231375));
#184112=CARTESIAN_POINT('Ctrl Pts',(16.6217706715984,19.3756377283516,4.49747292236368));
#184113=CARTESIAN_POINT('Ctrl Pts',(16.6354867602422,19.4922448590161,4.50419755621686));
#184114=CARTESIAN_POINT('Ctrl Pts',(16.6402991600693,19.5260763260431,4.5061771050553));
#184115=CARTESIAN_POINT('Ctrl Pts',(16.6476158018074,19.5698801127746,4.50878346735209));
#184116=CARTESIAN_POINT('Ctrl Pts',(16.6493769518854,19.5799724916309,4.50938697016501));
#184117=CARTESIAN_POINT('Ctrl Pts',(16.6524781189089,19.5970125896926,4.5104111770559));
#184118=CARTESIAN_POINT('Ctrl Pts',(16.6537798505403,19.6039671599484,4.51083066787339));
#184119=CARTESIAN_POINT('Ctrl Pts',(16.6564245897503,19.6177153434414,4.51166293430155));
#184120=CARTESIAN_POINT('Ctrl Pts',(16.657766117681,19.6245091534948,4.51207565819799));
#184121=CARTESIAN_POINT('Ctrl Pts',(16.6604207799739,19.6376143163115,4.51287464958691));
#184122=CARTESIAN_POINT('Ctrl Pts',(16.6617294578774,19.6439265011883,4.51326077048213));
#184123=CARTESIAN_POINT('Ctrl Pts',(16.6648077495934,19.658440307149,4.51415158556389));
#184124=CARTESIAN_POINT('Ctrl Pts',(16.6665973239782,19.6666375419306,4.51465691482729));
#184125=CARTESIAN_POINT('Ctrl Pts',(16.6715178769922,19.6885504292253,4.51601377451863));
#184126=CARTESIAN_POINT('Ctrl Pts',(16.6747368856452,19.702245693152,4.51686811845724));
#184127=CARTESIAN_POINT('Ctrl Pts',(16.6964948357784,19.7908407974831,4.52243687467858));
#184128=CARTESIAN_POINT('Ctrl Pts',(16.7189735904053,19.8646838242807,4.52727680304563));
#184129=CARTESIAN_POINT('Ctrl Pts',(16.7454193895773,19.9371102917951,4.53222340700496));
#184130=CARTESIAN_POINT('Origin',(18.734,19.211,0.));
#184131=CARTESIAN_POINT('',(16.7454193397875,19.9371101554369,5.55626850699162));
#184132=CARTESIAN_POINT('',(16.7454193775548,19.9371102588694,5.33540091894091));
#184133=CARTESIAN_POINT('',(16.7454193623258,19.9371102171621,0.));
#184134=CARTESIAN_POINT('Ctrl Pts',(16.7454193397875,19.9371101554369,5.55626850699162));
#184135=CARTESIAN_POINT('Ctrl Pts',(16.7359008819459,19.9110421807129,5.55474534815383));
#184136=CARTESIAN_POINT('Ctrl Pts',(16.7268931592987,19.8847819920176,5.55321402040514));
#184137=CARTESIAN_POINT('Ctrl Pts',(16.6925866569971,19.7779638736276,5.54697988012083));
#184138=CARTESIAN_POINT('Ctrl Pts',(16.6716050363402,19.6961196255081,5.54218747023461));
#184139=CARTESIAN_POINT('Ctrl Pts',(16.6528673383292,19.5993009577569,5.53639852339288));
#184140=CARTESIAN_POINT('Ctrl Pts',(16.6503087151907,19.5853279366274,5.5355603115109));
#184141=CARTESIAN_POINT('Ctrl Pts',(16.6465902595183,19.5638001875872,5.53426429491335));
#184142=CARTESIAN_POINT('Ctrl Pts',(16.6453303607485,19.5562629906949,5.53380967379834));
#184143=CARTESIAN_POINT('Ctrl Pts',(16.643106864124,19.5425034523681,5.53297809749433));
#184144=CARTESIAN_POINT('Ctrl Pts',(16.6421301614704,19.5362832948531,5.53260156320738));
#184145=CARTESIAN_POINT('Ctrl Pts',(16.6400580227851,19.5226914144666,5.53177741361028));
#184146=CARTESIAN_POINT('Ctrl Pts',(16.6389737391049,19.5153180995955,5.5313294499617));
#184147=CARTESIAN_POINT('Ctrl Pts',(16.6361094454234,19.4950992708156,5.53009858026596));
#184148=CARTESIAN_POINT('Ctrl Pts',(16.6344085220797,19.4822430437229,5.52931318575209));
#184149=CARTESIAN_POINT('Ctrl Pts',(16.6263685191507,19.416858900476,5.52530434253773));
#184150=CARTESIAN_POINT('Ctrl Pts',(16.6218825839194,19.3641260429436,5.52202306422395));
#184151=CARTESIAN_POINT('Ctrl Pts',(16.6177663610251,19.2773299077746,5.51653980109578));
#184152=CARTESIAN_POINT('Ctrl Pts',(16.6169742107429,19.2433434160845,5.51437224371054));
#184153=CARTESIAN_POINT('Ctrl Pts',(16.6171022078051,19.0787312575047,5.5037810304143));
#184154=CARTESIAN_POINT('Ctrl Pts',(16.6292932816139,18.9484055300888,5.49508949079167));
#184155=CARTESIAN_POINT('Ctrl Pts',(16.6709615176535,18.7266531037098,5.48023958195372));
#184156=CARTESIAN_POINT('Ctrl Pts',(16.6947819154142,18.6345335505787,5.4740597931356));
#184157=CARTESIAN_POINT('Ctrl Pts',(16.7277657519504,18.5351250513358,5.46758872593254));
#184158=CARTESIAN_POINT('Ctrl Pts',(16.7308789341621,18.5259534263594,5.46699363907557));
#184159=CARTESIAN_POINT('Ctrl Pts',(16.7355692047248,18.5124409982922,5.46612012492284));
#184160=CARTESIAN_POINT('Ctrl Pts',(16.7370976766334,18.5080836221592,5.46583893796131));
#184161=CARTESIAN_POINT('Ctrl Pts',(16.7398349366883,18.5003612139772,5.46534152791239));
#184162=CARTESIAN_POINT('Ctrl Pts',(16.7410380036105,18.496994211817,5.46512497056685));
#184163=CARTESIAN_POINT('Ctrl Pts',(16.743634281157,18.4897857444874,5.46466202601852));
#184164=CARTESIAN_POINT('Ctrl Pts',(16.745030081249,18.4859452709947,5.4644157954359));
#184165=CARTESIAN_POINT('Ctrl Pts',(16.7488929555607,18.4754118658669,5.46374152435155));
#184166=CARTESIAN_POINT('Ctrl Pts',(16.7513827768849,18.4687272530499,5.46331481829826));
#184167=CARTESIAN_POINT('Ctrl Pts',(16.7648702447291,18.4330684826696,5.46104432040453));
#184168=CARTESIAN_POINT('Ctrl Pts',(16.7764699587073,18.4043242258291,5.4592344139886));
#184169=CARTESIAN_POINT('Ctrl Pts',(16.8532264251643,18.2255379293045,5.44804382704229));
#184170=CARTESIAN_POINT('Ctrl Pts',(16.9349648113669,18.0832014923817,5.43939868918828));
#184171=CARTESIAN_POINT('Ctrl Pts',(17.1022876622664,17.8570979621112,5.42400417904076));
#184172=CARTESIAN_POINT('Ctrl Pts',(17.1800410611092,17.7685222165816,5.41743776600403));
#184173=CARTESIAN_POINT('Ctrl Pts',(17.2750386711216,17.676944803217,5.40970776342814));
#184174=CARTESIAN_POINT('Ctrl Pts',(17.2854344384217,17.6671245824852,5.40886563654019));
#184175=CARTESIAN_POINT('Ctrl Pts',(17.3021355840829,17.6516652608393,5.40751825127224));
#184176=CARTESIAN_POINT('Ctrl Pts',(17.3083767584939,17.6459572196154,5.40701593966362));
#184177=CARTESIAN_POINT('Ctrl Pts',(17.3194429388047,17.6359574552326,5.40612731634685));
#184178=CARTESIAN_POINT('Ctrl Pts',(17.3242537172059,17.6316500976897,5.40574167168038));
#184179=CARTESIAN_POINT('Ctrl Pts',(17.3342433775135,17.6227878084346,5.40494220223222));
#184180=CARTESIAN_POINT('Ctrl Pts',(17.3394249568205,17.618236045479,5.4045282516168));
#184181=CARTESIAN_POINT('Ctrl Pts',(17.3527797545426,17.6066196387535,5.40346316012071));
#184182=CARTESIAN_POINT('Ctrl Pts',(17.360984901458,17.5995921551588,5.40281049205809));
#184183=CARTESIAN_POINT('Ctrl Pts',(17.3954326846533,17.5705426922308,5.40007722057417));
#184184=CARTESIAN_POINT('Ctrl Pts',(17.4221529449053,17.5490975585353,5.39797334526817));
#184185=CARTESIAN_POINT('Ctrl Pts',(17.4930984235393,17.4949354732572,5.39242556030738));
#184186=CARTESIAN_POINT('Ctrl Pts',(17.5380970833765,17.4632787465323,5.38894338043964));
#184187=CARTESIAN_POINT('Ctrl Pts',(17.6611867536919,17.3836656152582,5.37952161406575));
#184188=CARTESIAN_POINT('Ctrl Pts',(17.7412415266193,17.3389669900743,5.37349485821874));
#184189=CARTESIAN_POINT('Ctrl Pts',(17.8723924390506,17.2765227868073,5.3638970371317));
#184190=CARTESIAN_POINT('Ctrl Pts',(17.9217125462298,17.2553009085088,5.36034697587555));
#184191=CARTESIAN_POINT('Ctrl Pts',(18.0061653416335,17.2227083585985,5.35441143042529));
#184192=CARTESIAN_POINT('Ctrl Pts',(18.0408861766309,17.2103400145177,5.3520108089968));
#184193=CARTESIAN_POINT('Ctrl Pts',(18.1208934790478,17.1841726711909,5.3465929024244));
#184194=CARTESIAN_POINT('Ctrl Pts',(18.1663581214309,17.1709725303705,5.34359556922666));
#184195=CARTESIAN_POINT('Ctrl Pts',(18.2196966717736,17.1574079193658,5.3402022895878));
#184196=CARTESIAN_POINT('Ctrl Pts',(18.2271731666627,17.1555499489859,5.33972943805029));
#184197=CARTESIAN_POINT('Ctrl Pts',(18.2391606598026,17.1526403426762,5.3389759282303));
#184198=CARTESIAN_POINT('Ctrl Pts',(18.2436651757001,17.1515626466134,5.33869382940661));
#184199=CARTESIAN_POINT('Ctrl Pts',(18.2516636875317,17.1496767497097,5.33819481569946));
#184200=CARTESIAN_POINT('Ctrl Pts',(18.2551562421806,17.1488626338585,5.33797756398594));
#184201=CARTESIAN_POINT('Ctrl Pts',(18.2625792611126,17.1471522008338,5.33751719855208));
#184202=CARTESIAN_POINT('Ctrl Pts',(18.2665102129466,17.1462582362916,5.33727422045448));
#184203=CARTESIAN_POINT('Ctrl Pts',(18.2771616051412,17.1438679085203,5.33661798594348));
#184204=CARTESIAN_POINT('Ctrl Pts',(18.2838868981239,17.1423930771809,5.33620594734778));
#184205=CARTESIAN_POINT('Ctrl Pts',(18.3177569515697,17.1351385020437,5.33414188419455));
#184206=CARTESIAN_POINT('Ctrl Pts',(18.3450076937946,17.129859834848,5.33251686239939));
#184207=CARTESIAN_POINT('Ctrl Pts',(18.4247510118996,17.1160341667165,5.32784450601));
#184208=CARTESIAN_POINT('Ctrl Pts',(18.477473609844,17.1089267939202,5.32485915066349));
#184209=CARTESIAN_POINT('Ctrl Pts',(18.6705416687809,17.0902732665784,5.31412753962805));
#184210=CARTESIAN_POINT('Ctrl Pts',(18.8116741229498,17.0907458170548,5.30664362646507));
#184211=CARTESIAN_POINT('Ctrl Pts',(19.0430902736284,17.1146721973172,5.29377453902092));
#184212=CARTESIAN_POINT('Ctrl Pts',(19.1337400752133,17.1300550382693,5.28858369472446));
#184213=CARTESIAN_POINT('Ctrl Pts',(19.2364890397762,17.1544535750968,5.28239262262585));
#184214=CARTESIAN_POINT('Ctrl Pts',(19.2498485700953,17.1577638537509,5.28158169977626));
#184215=CARTESIAN_POINT('Ctrl Pts',(19.2712122263524,17.1632790883111,5.28027496940906));
#184216=CARTESIAN_POINT('Ctrl Pts',(19.2792374479609,17.1654013026363,5.27978183387979));
#184217=CARTESIAN_POINT('Ctrl Pts',(19.2934589822938,17.1692517231672,5.27890383791887));
#184218=CARTESIAN_POINT('Ctrl Pts',(19.2996603222617,17.170961084384,5.27851959330443));
#184219=CARTESIAN_POINT('Ctrl Pts',(19.3125593944736,17.1745799715187,5.27771740349429));
#184220=CARTESIAN_POINT('Ctrl Pts',(19.3192556780933,17.1764943365059,5.27729930459204));
#184221=CARTESIAN_POINT('Ctrl Pts',(19.3366095470959,17.1815483069829,5.27621140438957));
#184222=CARTESIAN_POINT('Ctrl Pts',(19.34725197777,17.1847388014052,5.27553994776903));
#184223=CARTESIAN_POINT('Ctrl Pts',(19.3932530764568,17.1989250721566,5.27261866105073));
#184224=CARTESIAN_POINT('Ctrl Pts',(19.4283432210575,17.2107631755554,5.27034136810716));
#184225=CARTESIAN_POINT('Ctrl Pts',(19.5206296251234,17.2446181777198,5.2642173802715));
#184226=CARTESIAN_POINT('Ctrl Pts',(19.5772079639402,17.2682074572175,5.26032175831082));
#184227=CARTESIAN_POINT('Ctrl Pts',(19.7734704884578,17.3602246620092,5.24632255646222));
#184228=CARTESIAN_POINT('Ctrl Pts',(19.9065461192933,17.44153738527,5.23588749519248));
#184229=CARTESIAN_POINT('Ctrl Pts',(20.0418286309993,17.5462129905147,5.22476655187935));
#184230=CARTESIAN_POINT('Ctrl Pts',(20.0540398050925,17.555878721562,5.22375813015649));
#184231=CARTESIAN_POINT('Ctrl Pts',(20.1040093573971,17.5963368391654,5.2196158061706));
#184232=CARTESIAN_POINT('Ctrl Pts',(20.1408090014468,17.628295981744,5.21652733455363));
#184233=CARTESIAN_POINT('Ctrl Pts',(20.1821603104028,17.6667911302913,5.21304359419192));
#184234=CARTESIAN_POINT('Ctrl Pts',(20.1878157704311,17.6721143551931,5.21256684273039));
#184235=CARTESIAN_POINT('Ctrl Pts',(20.1968103011861,17.6806743336549,5.21180832655321));
#184236=CARTESIAN_POINT('Ctrl Pts',(20.2001681626347,17.6838911164694,5.21152509151034));
#184237=CARTESIAN_POINT('Ctrl Pts',(20.2060986058116,17.6896099866588,5.21102479143903));
#184238=CARTESIAN_POINT('Ctrl Pts',(20.2086754571095,17.692107582855,5.21080738343087));
#184239=CARTESIAN_POINT('Ctrl Pts',(20.2141260787188,17.6974175086571,5.21034748453693));
#184240=CARTESIAN_POINT('Ctrl Pts',(20.2169981854529,17.7002314705533,5.21010512519293));
#184241=CARTESIAN_POINT('Ctrl Pts',(20.2247329506738,17.707852959034,5.20945231296794));
#184242=CARTESIAN_POINT('Ctrl Pts',(20.2295804107833,17.7126759379944,5.20904305629049));
#184243=CARTESIAN_POINT('Ctrl Pts',(20.2535801101645,17.7367869501948,5.20701564236178));
#184244=CARTESIAN_POINT('Ctrl Pts',(20.2723839571762,17.7564200656637,5.20542335253164));
#184245=CARTESIAN_POINT('Ctrl Pts',(20.3257400308985,17.8143216813065,5.20087469686787));
#184246=CARTESIAN_POINT('Ctrl Pts',(20.3592806196731,17.8534985172206,5.19797646676236));
#184247=CARTESIAN_POINT('Ctrl Pts',(20.4769643503128,18.0015805239215,5.18749757438835));
#184248=CARTESIAN_POINT('Ctrl Pts',(20.551865596046,18.1173879606581,5.18017851917021));
#184249=CARTESIAN_POINT('Ctrl Pts',(20.6595464272297,18.3259094538104,5.16722919663671));
#184250=CARTESIAN_POINT('Ctrl Pts',(20.6981003208294,18.4151226120665,5.16175685041838));
#184251=CARTESIAN_POINT('Ctrl Pts',(20.735019797059,18.5197677698236,5.15525269135768));
#184252=CARTESIAN_POINT('Ctrl Pts',(20.7395152893983,18.532921365544,5.15443380410601));
#184253=CARTESIAN_POINT('Ctrl Pts',(20.7465005721551,18.5540372733794,5.15311668709294));
#184254=CARTESIAN_POINT('Ctrl Pts',(20.749073447548,18.5619718226137,5.15262119826229));
#184255=CARTESIAN_POINT('Ctrl Pts',(20.7535491497079,18.5760577273326,5.15174048946542));
#184256=CARTESIAN_POINT('Ctrl Pts',(20.7554709408655,18.582202980662,5.15135589841143));
#184257=CARTESIAN_POINT('Ctrl Pts',(20.7594076994409,18.5949960198031,5.1505544686821));
#184258=CARTESIAN_POINT('Ctrl Pts',(20.7614180387775,18.6016451388369,5.15013748365921));
#184259=CARTESIAN_POINT('Ctrl Pts',(20.7665352168011,18.6188756796934,5.14905569857016));
#184260=CARTESIAN_POINT('Ctrl Pts',(20.7695921326442,18.6294715995377,5.14838927790047));
#184261=CARTESIAN_POINT('Ctrl Pts',(20.7823462704288,18.6750132566875,5.14551961944914));
#184262=CARTESIAN_POINT('Ctrl Pts',(20.7912269607446,18.7101794639691,5.14329010684029));
#184263=CARTESIAN_POINT('Ctrl Pts',(20.812285091986,18.8036152629608,5.13732691457653));
#184264=CARTESIAN_POINT('Ctrl Pts',(20.8229152133099,18.8621971024793,5.13354743312624));
#184265=CARTESIAN_POINT('Ctrl Pts',(20.8541333448985,19.0880561249946,5.1188412943987));
#184266=CARTESIAN_POINT('Ctrl Pts',(20.8571927550826,19.2571060947732,5.10749629584318));
#184267=CARTESIAN_POINT('Ctrl Pts',(20.8347681008463,19.4780966419072,5.09313747102306));
#184268=CARTESIAN_POINT('Ctrl Pts',(20.8273244339242,19.5312516138185,5.08972633527414));
#184269=CARTESIAN_POINT('Ctrl Pts',(20.8163276155818,19.5926767452832,5.08587675846167));
#184270=CARTESIAN_POINT('Ctrl Pts',(20.8147335786007,19.6012732599647,5.0853401356639));
#184271=CARTESIAN_POINT('Ctrl Pts',(20.8122407122707,19.6142675099731,5.08453247331538));
#184272=CARTESIAN_POINT('Ctrl Pts',(20.8113811010626,19.6186725457341,5.08425928366856));
#184273=CARTESIAN_POINT('Ctrl Pts',(20.8098136987481,19.626570922788,5.08377057637449));
#184274=CARTESIAN_POINT('Ctrl Pts',(20.8091110913592,19.6300652250947,5.08355476890184));
#184275=CARTESIAN_POINT('Ctrl Pts',(20.8075661032799,19.6376498030672,5.08308722108849));
#184276=CARTESIAN_POINT('Ctrl Pts',(20.8067204466444,19.641739352605,5.08283567040323));
#184277=CARTESIAN_POINT('Ctrl Pts',(20.804313361678,19.6532086409666,5.08213165751559));
#184278=CARTESIAN_POINT('Ctrl Pts',(20.8027245665967,19.6605826610642,5.08168073226511));
#184279=CARTESIAN_POINT('Ctrl Pts',(20.7930399298121,19.7043930522184,5.07901103822222));
#184280=CARTESIAN_POINT('Ctrl Pts',(20.784020500265,19.7406210625401,5.07684184011556));
#184281=CARTESIAN_POINT('Ctrl Pts',(20.7513219864162,19.8585616835739,5.06985052443763));
#184282=CARTESIAN_POINT('Ctrl Pts',(20.7236754615083,19.9390920080005,5.06518734979452));
#184283=CARTESIAN_POINT('Ctrl Pts',(20.6233171252355,20.1825726637796,5.05085142417843));
#184284=CARTESIAN_POINT('Ctrl Pts',(20.5348400520287,20.3381384974425,5.04128048578719));
#184285=CARTESIAN_POINT('Ctrl Pts',(20.4142579818219,20.4989987847616,5.02959598716277));
#184286=CARTESIAN_POINT('Ctrl Pts',(20.4003040394721,20.5170009738923,5.02826143997338));
#184287=CARTESIAN_POINT('Ctrl Pts',(20.380115569651,20.5421960738657,5.02635334254832));
#184288=CARTESIAN_POINT('Ctrl Pts',(20.374118517069,20.5495778651999,5.02578927752239));
#184289=CARTESIAN_POINT('Ctrl Pts',(20.3642825316851,20.5615196755476,5.02486843869172));
#184290=CARTESIAN_POINT('Ctrl Pts',(20.3604736802066,20.5661043847744,5.02451288748692));
#184291=CARTESIAN_POINT('Ctrl Pts',(20.3524513615638,20.5756782900225,5.02376613093483));
#184292=CARTESIAN_POINT('Ctrl Pts',(20.348234074969,20.5806641904977,5.02337477136266));
#184293=CARTESIAN_POINT('Ctrl Pts',(20.3381296438044,20.5924986960532,5.02243990381693));
#184294=CARTESIAN_POINT('Ctrl Pts',(20.3322216470223,20.5993292564688,5.02189553761541));
#184295=CARTESIAN_POINT('Ctrl Pts',(20.3120895730855,20.6223062489225,5.0200479448339));
#184296=CARTESIAN_POINT('Ctrl Pts',(20.297663446107,20.6382731352455,5.0187362997404));
#184297=CARTESIAN_POINT('Ctrl Pts',(20.1601125469119,20.7859262285885,5.00633928592033));
#184298=CARTESIAN_POINT('Ctrl Pts',(20.0209042946421,20.901574252362,4.99450240301771));
#184299=CARTESIAN_POINT('Ctrl Pts',(19.8378303968496,21.0178178875436,4.98017594521599));
#184300=CARTESIAN_POINT('Ctrl Pts',(19.8063826533925,21.0366582239625,4.97775778460905));
#184301=CARTESIAN_POINT('Ctrl Pts',(19.7023683095064,21.0953578402881,4.96992584275602));
#184302=CARTESIAN_POINT('Ctrl Pts',(19.6279423707503,21.1317841683113,4.96457611118784));
#184303=CARTESIAN_POINT('Ctrl Pts',(19.5427055900718,21.1674704304197,4.95886775619578));
#184304=CARTESIAN_POINT('Ctrl Pts',(19.5338194325512,21.1711199350602,4.95827759503581));
#184305=CARTESIAN_POINT('Ctrl Pts',(19.520639595564,21.1764282807899,4.95740990645472));
#184306=CARTESIAN_POINT('Ctrl Pts',(19.5163649976677,21.1781337503042,4.95712967112614));
#184307=CARTESIAN_POINT('Ctrl Pts',(19.5087610876667,21.1811388351297,4.95663331104373));
#184308=CARTESIAN_POINT('Ctrl Pts',(19.5054340172229,21.1824439708978,4.95641685730301));
#184309=CARTESIAN_POINT('Ctrl Pts',(19.4982866676415,21.1852268530077,4.95595343095507));
#184310=CARTESIAN_POINT('Ctrl Pts',(19.4944654111288,21.1867019351617,4.95570661865175));
#184311=CARTESIAN_POINT('Ctrl Pts',(19.4839363224899,21.1907313026665,4.95502911153138));
#184312=CARTESIAN_POINT('Ctrl Pts',(19.47721967201,21.1932626064784,4.95459977257653));
#184313=CARTESIAN_POINT('Ctrl Pts',(19.44084965937,21.2067585254885,4.95228966477745));
#184314=CARTESIAN_POINT('Ctrl Pts',(19.4109646741078,21.2170926211615,4.95044419718279));
#184315=CARTESIAN_POINT('Ctrl Pts',(19.2252080429249,21.276702126775,4.93923155596619));
#184316=CARTESIAN_POINT('Ctrl Pts',(19.0642807074669,21.3084597640241,4.93059278410862));
#184317=CARTESIAN_POINT('Ctrl Pts',(18.7845695996124,21.3306321194186,4.91523325642181));
#184318=CARTESIAN_POINT('Ctrl Pts',(18.6673012266702,21.3301846532911,4.90869780898929));
#184319=CARTESIAN_POINT('Ctrl Pts',(18.5364402168657,21.3188101026219,4.90100265986646));
#184320=CARTESIAN_POINT('Ctrl Pts',(18.5222138389384,21.3174282336909,4.90016095812207));
#184321=CARTESIAN_POINT('Ctrl Pts',(18.499595443804,21.3149997629465,4.89881412604904));
#184322=CARTESIAN_POINT('Ctrl Pts',(18.4911936668189,21.3140467374377,4.89831193866344));
#184323=CARTESIAN_POINT('Ctrl Pts',(18.4763865460383,21.3122772308876,4.89742346006548));
#184324=CARTESIAN_POINT('Ctrl Pts',(18.4699787700267,21.3114817260348,4.89703783519828));
#184325=CARTESIAN_POINT('Ctrl Pts',(18.456733506889,21.3097758030101,4.89623833312042));
#184326=CARTESIAN_POINT('Ctrl Pts',(18.4498966371316,21.3088612577951,4.89582432971281));
#184327=CARTESIAN_POINT('Ctrl Pts',(18.4323598012534,21.306428115025,4.89475894724792));
#184328=CARTESIAN_POINT('Ctrl Pts',(18.4216668702656,21.3048609801094,4.89410603939718));
#184329=CARTESIAN_POINT('Ctrl Pts',(18.3770956153134,21.2979796918113,4.89137044558317));
#184330=CARTESIAN_POINT('Ctrl Pts',(18.3433384855378,21.2919248758422,4.88926443824005));
#184331=CARTESIAN_POINT('Ctrl Pts',(18.2557851028113,21.2740155084774,4.883709691274));
#184332=CARTESIAN_POINT('Ctrl Pts',(18.2022807515769,21.260877141984,4.88022256156937));
#184333=CARTESIAN_POINT('Ctrl Pts',(18.0415873592919,21.2147030748636,4.86947592303698));
#184334=CARTESIAN_POINT('Ctrl Pts',(17.9364595577411,21.175226779261,4.86205738668534));
#184335=CARTESIAN_POINT('Ctrl Pts',(17.7302656224575,21.0785061837106,4.84701617677167));
#184336=CARTESIAN_POINT('Ctrl Pts',(17.6297568832078,21.0208937693331,4.83942126725695));
#184337=CARTESIAN_POINT('Ctrl Pts',(17.5265596872077,20.9499274160579,4.83168481026389));
#184338=CARTESIAN_POINT('Ctrl Pts',(17.51870743511,20.9444487753917,4.83109662457768));
#184339=CARTESIAN_POINT('Ctrl Pts',(17.5071411558416,20.936261574281,4.83023127375603));
#184340=CARTESIAN_POINT('Ctrl Pts',(17.5033984731903,20.9335939760471,4.82995142134476));
#184341=CARTESIAN_POINT('Ctrl Pts',(17.4968468566269,20.9288920593997,4.82946186542343));
#184342=CARTESIAN_POINT('Ctrl Pts',(17.4940342072531,20.9268630077463,4.82925180501178));
#184343=CARTESIAN_POINT('Ctrl Pts',(17.4912136884051,20.9248177219187,4.82904127098932));
#184344=CARTESIAN_POINT('Ctrl Pts',(17.4912008812233,20.9248084346327,4.8290403150159));
#184345=CARTESIAN_POINT('Ctrl Pts',(17.4911754922149,20.9247900230455,4.82903841989492));
#184346=CARTESIAN_POINT('Ctrl Pts',(17.4911629101483,20.9247808985779,4.82903748072937));
#184347=CARTESIAN_POINT('Ctrl Pts',(17.4911379655358,20.9247628084192,4.82903561878836));
#184348=CARTESIAN_POINT('Ctrl Pts',(17.49112560336,20.9247538430037,4.82903469604046));
#184349=CARTESIAN_POINT('Ctrl Pts',(17.4911010934449,20.9247360672838,4.82903286655503));
#184350=CARTESIAN_POINT('Ctrl Pts',(17.4910889460705,20.924727257251,4.82903195984466));
#184351=CARTESIAN_POINT('Ctrl Pts',(17.4910648621215,20.9247097896798,4.82903016216265));
#184352=CARTESIAN_POINT('Ctrl Pts',(17.4910529252685,20.9247011319463,4.82902927117014));
#184353=CARTESIAN_POINT('Ctrl Pts',(17.4910292563409,20.9246839646264,4.82902750447416));
#184354=CARTESIAN_POINT('Ctrl Pts',(17.4910175247202,20.9246754553757,4.8290266288045));
#184355=CARTESIAN_POINT('Ctrl Pts',(17.4909942637492,20.924658583222,4.82902489256683));
#184356=CARTESIAN_POINT('Ctrl Pts',(17.4909827335356,20.924650219699,4.8290240319343));
#184357=CARTESIAN_POINT('Ctrl Pts',(17.4909598705549,20.9246336355199,4.82902232541063));
#184358=CARTESIAN_POINT('Ctrl Pts',(17.4909485375622,20.9246254147063,4.82902147950257));
#184359=CARTESIAN_POINT('Ctrl Pts',(17.4909260627822,20.9246091114369,4.82901980196182));
#184360=CARTESIAN_POINT('Ctrl Pts',(17.4909149219083,20.9246010296493,4.82901897039723));
#184361=CARTESIAN_POINT('Ctrl Pts',(17.4908928295068,20.9245850031006,4.82901732140444));
#184362=CARTESIAN_POINT('Ctrl Pts',(17.4908818774258,20.9245770579436,4.82901650393489));
#184363=CARTESIAN_POINT('Ctrl Pts',(17.4908601572638,20.924561300794,4.82901488273295));
#184364=CARTESIAN_POINT('Ctrl Pts',(17.4908493895367,20.9245534890635,4.82901407902693));
#184365=CARTESIAN_POINT('Ctrl Pts',(17.4908280346943,20.9245379963249,4.82901248509899));
#184366=CARTESIAN_POINT('Ctrl Pts',(17.4908174475402,20.9245303152938,4.82901169487413));
#184367=CARTESIAN_POINT('Ctrl Pts',(17.49079645014,20.924515081282,4.82901012763189));
#184368=CARTESIAN_POINT('Ctrl Pts',(17.4907860398119,20.9245075282469,4.82900935060835));
#184369=CARTESIAN_POINT('Ctrl Pts',(17.4907659469026,20.9244929499015,4.82900785088297));
#184370=CARTESIAN_POINT('Ctrl Pts',(17.4907562643268,20.9244859246146,4.82900712818133));
#184371=CARTESIAN_POINT('Ctrl Pts',(17.4907369361321,20.9244719006053,4.82900568553909));
#184372=CARTESIAN_POINT('Ctrl Pts',(17.4907272900563,20.9244649015522,4.82900496556438));
#184373=CARTESIAN_POINT('Ctrl Pts',(17.4907080349746,20.9244509300953,4.82900352838439));
#184374=CARTESIAN_POINT('Ctrl Pts',(17.4906984255579,20.9244439573942,4.82900281114845));
#184375=CARTESIAN_POINT('Ctrl Pts',(17.4906792409346,20.924430036569,4.82900137923252));
#184376=CARTESIAN_POINT('Ctrl Pts',(17.4906696668138,20.9244230892337,4.82900066463357));
#184377=CARTESIAN_POINT('Ctrl Pts',(17.490650555025,20.9244092207699,4.828999238159));
#184378=CARTESIAN_POINT('Ctrl Pts',(17.4906410168137,20.9244022992481,4.82899852624281));
#184379=CARTESIAN_POINT('Ctrl Pts',(17.487336924626,20.9220046015104,4.82875191474831));
#184380=CARTESIAN_POINT('Ctrl Pts',(17.4840492417595,20.9196043054218,4.82850667846364));
#184381=CARTESIAN_POINT('Ctrl Pts',(17.4772523840218,20.9146118873096,4.82799995013629));
#184382=CARTESIAN_POINT('Ctrl Pts',(17.4737442537365,20.9120183678084,4.8277385550803));
#184383=CARTESIAN_POINT('Ctrl Pts',(17.4648413934178,20.9053939275923,4.82707549844687));
#184384=CARTESIAN_POINT('Ctrl Pts',(17.4594577891916,20.9013480428791,4.82667483237144));
#184385=CARTESIAN_POINT('Ctrl Pts',(17.4439801747168,20.889600325604,4.82552347555291));
#184386=CARTESIAN_POINT('Ctrl Pts',(17.4339358474377,20.8818331509788,4.82477696000542));
#184387=CARTESIAN_POINT('Ctrl Pts',(17.3996896973846,20.8548551492021,4.82223168832354));
#184388=CARTESIAN_POINT('Ctrl Pts',(17.37583792717,20.8352043317,4.82045889576232));
#184389=CARTESIAN_POINT('Ctrl Pts',(17.2566464335356,20.7325433010826,4.81155040995274));
#184390=CARTESIAN_POINT('Ctrl Pts',(17.1684428879449,20.6416304561368,4.80477952094794));
#184391=CARTESIAN_POINT('Ctrl Pts',(17.0581895207994,20.5054980196726,4.79524214939786));
#184392=CARTESIAN_POINT('Ctrl Pts',(17.0288241449381,20.4665640012752,4.79257592184906));
#184393=CARTESIAN_POINT('Ctrl Pts',(16.948992145448,20.352746517156,4.78487975546769));
#184394=CARTESIAN_POINT('Ctrl Pts',(16.901940447921,20.2756093575782,4.77977469201102));
#184395=CARTESIAN_POINT('Ctrl Pts',(16.8535750200627,20.1835632133618,4.77367864978252));
#184396=CARTESIAN_POINT('Ctrl Pts',(16.847310418368,20.1713539547953,4.77287010304112));
#184397=CARTESIAN_POINT('Ctrl Pts',(16.8374528503508,20.1516734917865,4.77156647275801));
#184398=CARTESIAN_POINT('Ctrl Pts',(16.8337842369422,20.1442404619583,4.77107404079419));
#184399=CARTESIAN_POINT('Ctrl Pts',(16.8273471399922,20.1310028407844,4.77019685407985));
#184400=CARTESIAN_POINT('Ctrl Pts',(16.8245612602085,20.1252067890809,4.76981271123662));
#184401=CARTESIAN_POINT('Ctrl Pts',(16.8188109965202,20.11310235761,4.76901028530552));
#184402=CARTESIAN_POINT('Ctrl Pts',(16.815851276527,20.1067918594664,4.76859184628077));
#184403=CARTESIAN_POINT('Ctrl Pts',(16.808244173595,20.0903619825484,4.76750207988746));
#184404=CARTESIAN_POINT('Ctrl Pts',(16.8036454185036,20.0802204447428,4.76682908655037));
#184405=CARTESIAN_POINT('Ctrl Pts',(16.7840055964983,20.0359845319037,4.76389185826396));
#184406=CARTESIAN_POINT('Ctrl Pts',(16.7697869657525,20.001534332524,4.76159978792033));
#184407=CARTESIAN_POINT('Ctrl Pts',(16.7527228285433,19.9568826108312,4.75862125090952));
#184408=CARTESIAN_POINT('Ctrl Pts',(16.7490340127606,19.9470095736933,4.75796219637102));
#184409=CARTESIAN_POINT('Ctrl Pts',(16.745419360568,19.9371102123481,4.75730092050388));
#184410=CARTESIAN_POINT('Ctrl Pts',(16.7454193895773,19.9371102917951,4.53222340700496));
#184411=CARTESIAN_POINT('Ctrl Pts',(16.7547724031316,19.9627251627221,4.5339728589152));
#184412=CARTESIAN_POINT('Ctrl Pts',(16.7646216281624,19.9881628702676,4.53573529112474));
#184413=CARTESIAN_POINT('Ctrl Pts',(16.8069143125145,20.0914181420184,4.54298757155657));
#184414=CARTESIAN_POINT('Ctrl Pts',(16.8434960439116,20.1674460000309,4.54856267278766));
#184415=CARTESIAN_POINT('Ctrl Pts',(16.9297171882361,20.3222534345793,4.5602691081327));
#184416=CARTESIAN_POINT('Ctrl Pts',(16.9802211974873,20.4003624888217,4.56638699544503));
#184417=CARTESIAN_POINT('Ctrl Pts',(17.0541350598679,20.4996801506508,4.57424155302913));
#184418=CARTESIAN_POINT('Ctrl Pts',(17.0731139875003,20.5240501261232,4.5761749357766));
#184419=CARTESIAN_POINT('Ctrl Pts',(17.0971204775874,20.5535219546146,4.57851181434706));
#184420=CARTESIAN_POINT('Ctrl Pts',(17.101648400782,20.5590237495591,4.57894800520774));
#184421=CARTESIAN_POINT('Ctrl Pts',(17.1088155012202,20.5676432942862,4.5796311420402));
#184422=CARTESIAN_POINT('Ctrl Pts',(17.1114360225727,20.5707763870626,4.57987940431196));
#184423=CARTESIAN_POINT('Ctrl Pts',(17.1163676776681,20.5766381131326,4.58034375514298));
#184424=CARTESIAN_POINT('Ctrl Pts',(17.1186766300381,20.5793684434234,4.58055998973853));
#184425=CARTESIAN_POINT('Ctrl Pts',(17.1239849536179,20.5856133631342,4.58105446202591));
#184426=CARTESIAN_POINT('Ctrl Pts',(17.126988915279,20.5891239865106,4.58133235742921));
#184427=CARTESIAN_POINT('Ctrl Pts',(17.134898392322,20.5983064843049,4.58205911693098));
#184428=CARTESIAN_POINT('Ctrl Pts',(17.1398226420926,20.6039622350875,4.58250663461414));
#184429=CARTESIAN_POINT('Ctrl Pts',(17.1733079994211,20.6420117237219,4.58551752225174));
#184430=CARTESIAN_POINT('Ctrl Pts',(17.2028266717027,20.6735535495631,4.58801438268116));
#184431=CARTESIAN_POINT('Ctrl Pts',(17.2842045091331,20.7553420801205,4.59456222978682));
#184432=CARTESIAN_POINT('Ctrl Pts',(17.3377044100379,20.8038777115785,4.59852795480883));
#184433=CARTESIAN_POINT('Ctrl Pts',(17.4624081722022,20.9058893944541,4.60730940827461));
#184434=CARTESIAN_POINT('Ctrl Pts',(17.534711715258,20.9577980077863,4.61210237594066));
#184435=CARTESIAN_POINT('Ctrl Pts',(17.6709782681035,21.0431682831148,4.62094043598707));
#184436=CARTESIAN_POINT('Ctrl Pts',(17.7337916214673,21.0782005235154,4.62494614642702));
#184437=CARTESIAN_POINT('Ctrl Pts',(17.822789608461,21.1220552925393,4.63062060121498));
#184438=CARTESIAN_POINT('Ctrl Pts',(17.8475487036928,21.1336650026921,4.63219883417538));
#184439=CARTESIAN_POINT('Ctrl Pts',(17.8907913189896,21.1529289372445,4.63495900587287));
#184440=CARTESIAN_POINT('Ctrl Pts',(17.90917157596,21.160806889793,4.63613334678326));
#184441=CARTESIAN_POINT('Ctrl Pts',(17.9357429790224,21.1717526987597,4.63783378020182));
#184442=CARTESIAN_POINT('Ctrl Pts',(17.9438461872591,21.1750321702946,4.63835270503047));
#184443=CARTESIAN_POINT('Ctrl Pts',(17.9580191020464,21.1806662226505,4.63926105522602));
#184444=CARTESIAN_POINT('Ctrl Pts',(17.9640798291557,21.1830431820084,4.63964972040308));
#184445=CARTESIAN_POINT('Ctrl Pts',(17.9757324035469,21.1875513052105,4.6403974615899));
#184446=CARTESIAN_POINT('Ctrl Pts',(17.9813225198315,21.1896867917042,4.64075638784115));
#184447=CARTESIAN_POINT('Ctrl Pts',(17.9959422523476,21.1952007733782,4.64169566810272));
#184448=CARTESIAN_POINT('Ctrl Pts',(18.0049859501767,21.1985413098335,4.64227728532399));
#184449=CARTESIAN_POINT('Ctrl Pts',(18.0362110509937,21.2098333647504,4.64428761315423));
#184450=CARTESIAN_POINT('Ctrl Pts',(18.0585015738364,21.2174760260821,4.64572651785464));
#184451=CARTESIAN_POINT('Ctrl Pts',(18.2398094051443,21.2762766970307,4.65746513332573));
#184452=CARTESIAN_POINT('Ctrl Pts',(18.40421679544,21.3088119272805,4.66839452133173));
#184453=CARTESIAN_POINT('Ctrl Pts',(18.6959959875962,21.331386176601,4.68773428716091));
#184454=CARTESIAN_POINT('Ctrl Pts',(18.8219189870175,21.3299050765897,4.69603952767565));
#184455=CARTESIAN_POINT('Ctrl Pts',(18.9588894693142,21.3160551248909,4.70457755196367));
#184456=CARTESIAN_POINT('Ctrl Pts',(18.9707915911399,21.3147495359008,4.70531519899863));
#184457=CARTESIAN_POINT('Ctrl Pts',(18.9876810792895,21.3127517092587,4.70635526248402));
#184458=CARTESIAN_POINT('Ctrl Pts',(18.9926777868767,21.3121425799167,4.7066621301672));
#184459=CARTESIAN_POINT('Ctrl Pts',(19.0012794044883,21.3110628409443,4.70718890010166));
#184460=CARTESIAN_POINT('Ctrl Pts',(19.0048853465937,21.3106007586581,4.70740927891704));
#184461=CARTESIAN_POINT('Ctrl Pts',(19.0118701489965,21.3096873993242,4.70783526238312));
#184462=CARTESIAN_POINT('Ctrl Pts',(19.0152491096885,21.3092372502806,4.70804093187515));
#184463=CARTESIAN_POINT('Ctrl Pts',(19.0243530967718,21.3080020197958,4.70859401717607));
#184464=CARTESIAN_POINT('Ctrl Pts',(19.0300760689755,21.3072016494114,4.70894057576158));
#184465=CARTESIAN_POINT('Ctrl Pts',(19.0512492589261,21.3041520900465,4.71021880974948));
#184466=CARTESIAN_POINT('Ctrl Pts',(19.0666781637117,21.3017553744563,4.71114251818596));
#184467=CARTESIAN_POINT('Ctrl Pts',(19.2162896517319,21.2768166665044,4.7200365213711));
#184468=CARTESIAN_POINT('Ctrl Pts',(19.3480498235207,21.2415553121407,4.72738866559904));
#184469=CARTESIAN_POINT('Ctrl Pts',(19.6208175470008,21.1395499936416,4.74320315406878));
#184470=CARTESIAN_POINT('Ctrl Pts',(19.7596770207882,21.069421268459,4.75165213867748));
#184471=CARTESIAN_POINT('Ctrl Pts',(19.9074470201853,20.9731474323135,4.76192312587365));
#184472=CARTESIAN_POINT('Ctrl Pts',(19.9250932403537,20.9612680727889,4.76317138994192));
#184473=CARTESIAN_POINT('Ctrl Pts',(19.9499376788251,20.943993183069,4.76496143526196));
#184474=CARTESIAN_POINT('Ctrl Pts',(19.95728550718,20.9388143347817,4.76549497927053));
#184475=CARTESIAN_POINT('Ctrl Pts',(19.9699075504003,20.929797275118,4.7664187626107));
#184476=CARTESIAN_POINT('Ctrl Pts',(19.97519745931,20.9259811694662,4.76680814775332));
#184477=CARTESIAN_POINT('Ctrl Pts',(19.9852943117695,20.9186261813015,4.76755568547137));
#184478=CARTESIAN_POINT('Ctrl Pts',(19.9901040962707,20.9150912909615,4.76791368066152));
#184479=CARTESIAN_POINT('Ctrl Pts',(20.0025768158454,20.9058431266994,4.76884701356077));
#184480=CARTESIAN_POINT('Ctrl Pts',(20.0102160580531,20.9000982595164,4.76942358334729));
#184481=CARTESIAN_POINT('Ctrl Pts',(20.0361560255342,20.8803144372035,4.77139846675003));
#184482=CARTESIAN_POINT('Ctrl Pts',(20.0542655948021,20.8660286094909,4.77280649815665));
#184483=CARTESIAN_POINT('Ctrl Pts',(20.2073526595561,20.7411534018292,4.78496747018673));
#184484=CARTESIAN_POINT('Ctrl Pts',(20.3283879088352,20.6145817154827,4.79641511794876));
#184485=CARTESIAN_POINT('Ctrl Pts',(20.4848585158912,20.4042629949358,4.81373572183579));
#184486=CARTESIAN_POINT('Ctrl Pts',(20.5327921438261,20.3307012440144,4.81951808435455));
#184487=CARTESIAN_POINT('Ctrl Pts',(20.5947541723614,20.2213102731512,4.82754600037828));
#184488=CARTESIAN_POINT('Ctrl Pts',(20.612590037135,20.1877460395428,4.82993653044006));
#184489=CARTESIAN_POINT('Ctrl Pts',(20.6328900472641,20.1469289886025,4.83274178313648));
#184490=CARTESIAN_POINT('Ctrl Pts',(20.6362298399888,20.1401222326234,4.83320625804087));
#184491=CARTESIAN_POINT('Ctrl Pts',(20.6413560478656,20.1295311187441,4.83392363258702));
#184492=CARTESIAN_POINT('Ctrl Pts',(20.6431678931797,20.1257592392439,4.8341780713481));
#184493=CARTESIAN_POINT('Ctrl Pts',(20.6465020166357,20.1187652423503,4.8346478981996));
#184494=CARTESIAN_POINT('Ctrl Pts',(20.6480273297439,20.1155446811237,4.8348634692277));
#184495=CARTESIAN_POINT('Ctrl Pts',(20.6514506913586,20.1082691295567,4.83534873537581));
#184496=CARTESIAN_POINT('Ctrl Pts',(20.6533440072738,20.1042119721746,4.83561813643903));
#184497=CARTESIAN_POINT('Ctrl Pts',(20.6588751328043,20.0922606163445,4.8364082750482));
#184498=CARTESIAN_POINT('Ctrl Pts',(20.66247726278,20.0843498746848,4.8369268647328));
#184499=CARTESIAN_POINT('Ctrl Pts',(20.6875903738253,20.0282852273785,4.84057263600805));
#184500=CARTESIAN_POINT('Ctrl Pts',(20.7073459139531,19.979360191637,4.8436007460277));
#184501=CARTESIAN_POINT('Ctrl Pts',(20.7306239365612,19.9148692673999,4.84745858327113));
#184502=CARTESIAN_POINT('Ctrl Pts',(20.7358262865938,19.8999344131664,4.84834285558233));
#184503=CARTESIAN_POINT('Ctrl Pts',(20.7570370098401,19.8367732732829,4.85204951361411));
#184504=CARTESIAN_POINT('Ctrl Pts',(20.7714741991618,19.7880356728824,4.85482939570848));
#184505=CARTESIAN_POINT('Ctrl Pts',(20.8114224450757,19.6328710624809,4.86355299253518));
#184506=CARTESIAN_POINT('Ctrl Pts',(20.8304458556555,19.5249635426065,4.86944395434718));
#184507=CARTESIAN_POINT('Ctrl Pts',(20.8463892184264,19.3611523036757,4.87859496729409));
#184508=CARTESIAN_POINT('Ctrl Pts',(20.8495848999776,19.306046346207,4.88170631117984));
#184509=CARTESIAN_POINT('Ctrl Pts',(20.851271223758,19.2165476221695,4.88685609271407));
#184510=CARTESIAN_POINT('Ctrl Pts',(20.851082629538,19.1822049718464,4.88885502671365));
#184511=CARTESIAN_POINT('Ctrl Pts',(20.84973654013,19.137075681761,4.89151775727164));
#184512=CARTESIAN_POINT('Ctrl Pts',(20.849331380304,19.1262706839147,4.89215797844407));
#184513=CARTESIAN_POINT('Ctrl Pts',(20.8485321514039,19.1085774604239,4.89321094859615));
#184514=CARTESIAN_POINT('Ctrl Pts',(20.8481871467756,19.1016871342869,4.89362215477677));
#184515=CARTESIAN_POINT('Ctrl Pts',(20.847454076057,19.0883519063292,4.89442025010244));
#184516=CARTESIAN_POINT('Ctrl Pts',(20.8470701933843,19.0819068441732,4.89480700353001));
#184517=CARTESIAN_POINT('Ctrl Pts',(20.8461156684166,19.0670282942449,4.89570224216919));
#184518=CARTESIAN_POINT('Ctrl Pts',(20.8455239900448,19.0585963089127,4.89621138286472));
#184519=CARTESIAN_POINT('Ctrl Pts',(20.8437967253615,19.0359263433742,4.89758515815393));
#184520=CARTESIAN_POINT('Ctrl Pts',(20.8425675317957,19.0216961285327,4.89845271728173));
#184521=CARTESIAN_POINT('Ctrl Pts',(20.8276340102067,18.8670784543557,4.90793751289946));
#184522=CARTESIAN_POINT('Ctrl Pts',(20.800078219931,18.7284102787073,4.91700442466364));
#184523=CARTESIAN_POINT('Ctrl Pts',(20.7307663204369,18.5011051192184,4.93263823563054));
#184524=CARTESIAN_POINT('Ctrl Pts',(20.6962868452609,18.4107144161009,4.93906604169451));
#184525=CARTESIAN_POINT('Ctrl Pts',(20.6352164816006,18.2785505635589,4.94856667560684));
#184526=CARTESIAN_POINT('Ctrl Pts',(20.6131425756001,18.2348289723727,4.9517261918189));
#184527=CARTESIAN_POINT('Ctrl Pts',(20.5769352273177,18.1689022368994,4.95647581505038));
#184528=CARTESIAN_POINT('Ctrl Pts',(20.5638719655971,18.1461306483408,4.95811352970189));
#184529=CARTESIAN_POINT('Ctrl Pts',(20.5469161901493,18.1178076244426,4.96014129394114));
#184530=CARTESIAN_POINT('Ctrl Pts',(20.5434166961062,18.1120250661705,4.96055479985511));
#184531=CARTESIAN_POINT('Ctrl Pts',(20.5378004520503,18.1028443452635,4.96121039597595));
#184532=CARTESIAN_POINT('Ctrl Pts',(20.535701687957,18.0994353126474,4.96145363432592));
#184533=CARTESIAN_POINT('Ctrl Pts',(20.5317008918475,18.0929779012346,4.9619139649244));
#184534=CARTESIAN_POINT('Ctrl Pts',(20.5298007934423,18.0899284499628,4.96213117210257));
#184535=CARTESIAN_POINT('Ctrl Pts',(20.5254067744917,18.0829163641073,4.96263024086052));
#184536=CARTESIAN_POINT('Ctrl Pts',(20.5229074662741,18.0789571565812,4.9629117425935));
#184537=CARTESIAN_POINT('Ctrl Pts',(20.5161686509784,18.0683601036956,4.96366452260831));
#184538=CARTESIAN_POINT('Ctrl Pts',(20.5119051549568,18.0617374984379,4.96413425617177));
#184539=CARTESIAN_POINT('Ctrl Pts',(20.4795578579187,18.0121023734511,4.96765064419475));
#184540=CARTESIAN_POINT('Ctrl Pts',(20.4499513632432,17.970097266647,4.9706029164804));
#184541=CARTESIAN_POINT('Ctrl Pts',(20.4053233164184,17.9114362331128,4.97475500542819));
#184542=CARTESIAN_POINT('Ctrl Pts',(20.3915226035269,17.8938794741043,4.97600161911873));
#184543=CARTESIAN_POINT('Ctrl Pts',(20.3484989233046,17.8408937569714,4.97978676898204));
#184544=CARTESIAN_POINT('Ctrl Pts',(20.3183982674685,17.8061938704881,4.98229791694414));
#184545=CARTESIAN_POINT('Ctrl Pts',(20.2128871495548,17.6922703497104,4.99075189548715));
#184546=CARTESIAN_POINT('Ctrl Pts',(20.1324782965989,17.617919800404,4.99664011503158));
#184547=CARTESIAN_POINT('Ctrl Pts',(20.0034505804157,17.5159419791502,5.00578475207915));
#184548=CARTESIAN_POINT('Ctrl Pts',(19.9588963326422,17.4834714766529,5.00889244094536));
#184549=CARTESIAN_POINT('Ctrl Pts',(19.8846336801858,17.4336682225758,5.0140367120459));
#184550=CARTESIAN_POINT('Ctrl Pts',(19.8556800741764,17.4152551050896,5.01603390139742));
#184551=CARTESIAN_POINT('Ctrl Pts',(19.8170338138094,17.3919772969146,5.01869463708521));
#184552=CARTESIAN_POINT('Ctrl Pts',(19.8077321923982,17.3864712913622,5.01933465309387));
#184553=CARTESIAN_POINT('Ctrl Pts',(19.7924260363541,17.3775685420849,5.02038737173758));
#184554=CARTESIAN_POINT('Ctrl Pts',(19.7864462696531,17.3741294457512,5.02079853301977));
#184555=CARTESIAN_POINT('Ctrl Pts',(19.7748370282912,17.3675280118672,5.02159660261079));
#184556=CARTESIAN_POINT('Ctrl Pts',(19.7692096780856,17.3643620789506,5.02198337552727));
#184557=CARTESIAN_POINT('Ctrl Pts',(19.7561805459115,17.3571101941001,5.02287874872795));
#184558=CARTESIAN_POINT('Ctrl Pts',(19.7487686313392,17.3530427608607,5.02338800511676));
#184559=CARTESIAN_POINT('Ctrl Pts',(19.7287643488092,17.3422204290836,5.02476229501168));
#184560=CARTESIAN_POINT('Ctrl Pts',(19.7161277915873,17.3355485397878,5.02563025646234));
#184561=CARTESIAN_POINT('Ctrl Pts',(19.5995665721896,17.2755072745005,5.0336362051208));
#184562=CARTESIAN_POINT('Ctrl Pts',(19.4914753091594,17.2307068564076,5.04107585443661));
#184563=CARTESIAN_POINT('Ctrl Pts',(19.225366708625,17.145399820272,5.05932908809907));
#184564=CARTESIAN_POINT('Ctrl Pts',(19.0652748172525,17.1137631505918,5.07028255410712));
#184565=CARTESIAN_POINT('Ctrl Pts',(18.8706538886571,17.0981637836033,5.08268982397046));
#184566=CARTESIAN_POINT('Ctrl Pts',(18.8381093147782,17.0963102630211,5.08473259130549));
#184567=CARTESIAN_POINT('Ctrl Pts',(18.7982917953702,17.0949640694958,5.08718250958665));
#184568=CARTESIAN_POINT('Ctrl Pts',(18.791049318659,17.0947564240208,5.08762613395383));
#184569=CARTESIAN_POINT('Ctrl Pts',(18.7796960202292,17.0944892456281,5.08831828107385));
#184570=CARTESIAN_POINT('Ctrl Pts',(18.7755859278407,17.0944044999324,5.08856817726714));
#184571=CARTESIAN_POINT('Ctrl Pts',(18.767904427225,17.0942684990994,5.08903392629171));
#184572=CARTESIAN_POINT('Ctrl Pts',(18.764333175357,17.0942143103766,5.08924993504588));
#184573=CARTESIAN_POINT('Ctrl Pts',(18.7561826254542,17.0941112682525,5.08974174246457));
#184574=CARTESIAN_POINT('Ctrl Pts',(18.7516033043237,17.0940682353811,5.09001721258166));
#184575=CARTESIAN_POINT('Ctrl Pts',(18.737534086303,17.0939816796058,5.09086104268522));
#184576=CARTESIAN_POINT('Ctrl Pts',(18.7280438570151,17.0939871066532,5.09142673467748));
#184577=CARTESIAN_POINT('Ctrl Pts',(18.6431550663979,17.0946064950797,5.09645796986016));
#184578=CARTESIAN_POINT('Ctrl Pts',(18.5678307116975,17.0991845255335,5.10071979605209));
#184579=CARTESIAN_POINT('Ctrl Pts',(18.4500663849144,17.1126840444024,5.10728229417409));
#184580=CARTESIAN_POINT('Ctrl Pts',(18.4073879595804,17.1189022693486,5.10963942608538));
#184581=CARTESIAN_POINT('Ctrl Pts',(18.2572775361348,17.1454790906703,5.11793904403986));
#184582=CARTESIAN_POINT('Ctrl Pts',(18.1512660163912,17.1728485943846,5.12382591689914));
#184583=CARTESIAN_POINT('Ctrl Pts',(17.9957398930832,17.2261335489584,5.13296742314825));
#184584=CARTESIAN_POINT('Ctrl Pts',(17.9443529376154,17.2460115302313,5.13607331751969));
#184585=CARTESIAN_POINT('Ctrl Pts',(17.8623244775952,17.2814801460156,5.1412148829299));
#184586=CARTESIAN_POINT('Ctrl Pts',(17.8311837804071,17.295853070767,5.14321121540479));
#184587=CARTESIAN_POINT('Ctrl Pts',(17.7907074571016,17.3157414483959,5.14587097127644));
#184588=CARTESIAN_POINT('Ctrl Pts',(17.7810445468789,17.3205816080224,5.14651088645943));
#184589=CARTESIAN_POINT('Ctrl Pts',(17.7652757054991,17.3286318581835,5.14756348150383));
#184590=CARTESIAN_POINT('Ctrl Pts',(17.7591475790864,17.3317982184476,5.14797462072292));
#184591=CARTESIAN_POINT('Ctrl Pts',(17.7473131683997,17.3379864419036,5.14877267768463));
#184592=CARTESIAN_POINT('Ctrl Pts',(17.741605013278,17.3410045771814,5.14915946019479));
#184593=CARTESIAN_POINT('Ctrl Pts',(17.7284539628243,17.3480352489271,5.1500548995994));
#184594=CARTESIAN_POINT('Ctrl Pts',(17.7210211588868,17.3520663376988,5.15056421290376));
#184595=CARTESIAN_POINT('Ctrl Pts',(17.7010897570283,17.3630309211966,5.15193875598499));
#184596=CARTESIAN_POINT('Ctrl Pts',(17.6886370645698,17.3700465503574,5.15280691538503));
#184597=CARTESIAN_POINT('Ctrl Pts',(17.574844574266,17.4356820841356,5.16082808391067));
#184598=CARTESIAN_POINT('Ctrl Pts',(17.4784761341347,17.5024781312564,5.16828408716822));
#184599=CARTESIAN_POINT('Ctrl Pts',(17.2619797984708,17.6807857422063,5.18660583212604));
#184600=CARTESIAN_POINT('Ctrl Pts',(17.1482848611456,17.7989423417665,5.19761347861307));
#184601=CARTESIAN_POINT('Ctrl Pts',(17.0301307043909,17.9542096716946,5.21000153862169));
#184602=CARTESIAN_POINT('Ctrl Pts',(17.011514269283,17.9798478310744,5.21198583008886));
#184603=CARTESIAN_POINT('Ctrl Pts',(16.9893908034225,18.0118005448169,5.21437540053925));
#184604=CARTESIAN_POINT('Ctrl Pts',(16.9853324120053,18.0177262459109,5.21481510907938));
#184605=CARTESIAN_POINT('Ctrl Pts',(16.9790063682987,18.0270645549086,5.21550251074813));
#184606=CARTESIAN_POINT('Ctrl Pts',(16.9767183761698,18.0304632235029,5.21575154709066));
#184607=CARTESIAN_POINT('Ctrl Pts',(16.9724530902216,18.0368389137305,5.21621655535392));
#184608=CARTESIAN_POINT('Ctrl Pts',(16.9704734906456,18.0398142662742,5.21643267800726));
#184609=CARTESIAN_POINT('Ctrl Pts',(16.965962634248,18.0466314846174,5.21692586518573));
#184610=CARTESIAN_POINT('Ctrl Pts',(16.9634363651837,18.0504765912347,5.21720259403024));
#184611=CARTESIAN_POINT('Ctrl Pts',(16.9568611826751,18.0605557899601,5.21792430339818));
#184612=CARTESIAN_POINT('Ctrl Pts',(16.9528324936584,18.0668030875385,5.21836796768994));
#184613=CARTESIAN_POINT('Ctrl Pts',(16.926302248451,18.1084232971088,5.22130035610816));
#184614=CARTESIAN_POINT('Ctrl Pts',(16.9048211309003,18.1444392942485,5.22372644549766));
#184615=CARTESIAN_POINT('Ctrl Pts',(16.8738463903104,18.2000647307905,5.22734415302085));
#184616=CARTESIAN_POINT('Ctrl Pts',(16.8635633226522,18.2192196524102,5.22856741894502));
#184617=CARTESIAN_POINT('Ctrl Pts',(16.8457315551936,18.2537001718309,5.23073542111984));
#184618=CARTESIAN_POINT('Ctrl Pts',(16.8380699937973,18.268964909688,5.23168355708691));
#184619=CARTESIAN_POINT('Ctrl Pts',(16.7722507276487,18.4041582023236,5.23999251826942));
#184620=CARTESIAN_POINT('Ctrl Pts',(16.7253544921118,18.5292383492191,5.24709266696999));
#184621=CARTESIAN_POINT('Ctrl Pts',(16.6648838067213,18.7526521436461,5.25986483911706));
#184622=CARTESIAN_POINT('Ctrl Pts',(16.6458617353918,18.8490613194394,5.26540003990553));
#184623=CARTESIAN_POINT('Ctrl Pts',(16.6317631834271,18.9609907874177,5.27201864742314));
#184624=CARTESIAN_POINT('Ctrl Pts',(16.6300811152861,18.9755651902119,5.27288398401178));
#184625=CARTESIAN_POINT('Ctrl Pts',(16.627743251156,18.9978535302092,5.27421314617396));
#184626=CARTESIAN_POINT('Ctrl Pts',(16.6269780363235,19.005555720974,5.27467352386008));
#184627=CARTESIAN_POINT('Ctrl Pts',(16.6257184970672,19.018981494221,5.27547792086462));
#184628=CARTESIAN_POINT('Ctrl Pts',(16.6252051970251,19.0247032471825,5.27582133899206));
#184629=CARTESIAN_POINT('Ctrl Pts',(16.6241033853434,19.0375735783999,5.27659519862606));
#184630=CARTESIAN_POINT('Ctrl Pts',(16.6235279049997,19.0447231750921,5.27702604581187));
#184631=CARTESIAN_POINT('Ctrl Pts',(16.6220830311232,19.0638914665212,5.27818379777301));
#184632=CARTESIAN_POINT('Ctrl Pts',(16.6212799116562,19.0759147567252,5.27891277405855));
#184633=CARTESIAN_POINT('Ctrl Pts',(16.6181723376119,19.1292856913703,5.28216140879962));
#184634=CARTESIAN_POINT('Ctrl Pts',(16.6169788915335,19.1706865691505,5.28471558063671));
#184635=CARTESIAN_POINT('Ctrl Pts',(16.6170878346041,19.3815723324421,5.29790820293532));
#184636=CARTESIAN_POINT('Ctrl Pts',(16.6375272207745,19.5504051819816,5.30913937631477));
#184637=CARTESIAN_POINT('Ctrl Pts',(16.6963015727514,19.7902026215764,5.325418800653));
#184638=CARTESIAN_POINT('Ctrl Pts',(16.7188568487697,19.8643641030618,5.33048898654639));
#184639=CARTESIAN_POINT('Ctrl Pts',(16.7454193775548,19.9371102588694,5.3354009189409));
#184640=CARTESIAN_POINT('Origin',(18.734,19.211,0.));
#184641=CARTESIAN_POINT('',(16.7454193623257,19.9371102171619,6.35350368608372));
#184642=CARTESIAN_POINT('',(16.7454193623258,19.9371102171621,6.13370787675019));
#184643=CARTESIAN_POINT('',(16.7454193623258,19.9371102171621,0.));
#184644=CARTESIAN_POINT('',(16.6170004208961,19.2123349433974,6.31236855845777));
#184645=CARTESIAN_POINT('Ctrl Pts',(16.7454193623257,19.9371102171619,6.35350368608372));
#184646=CARTESIAN_POINT('Ctrl Pts',(16.7415068896361,19.9263952220385,6.3528225148824));
#184647=CARTESIAN_POINT('Ctrl Pts',(16.7376809777106,19.9156484895932,6.35214624380759));
#184648=CARTESIAN_POINT('Ctrl Pts',(16.7125808673215,19.8432983391641,6.34763638594729));
#184649=CARTESIAN_POINT('Ctrl Pts',(16.6940722989538,19.7807658436308,6.34394655327977));
#184650=CARTESIAN_POINT('Ctrl Pts',(16.6377481840861,19.5521743616963,6.33087426327147));
#184651=CARTESIAN_POINT('Ctrl Pts',(16.6171077708269,19.3825741900344,6.32190080849233));
#184652=CARTESIAN_POINT('Ctrl Pts',(16.6170004208961,19.2123349433974,6.31236855845777));
#184653=CARTESIAN_POINT('Ctrl Pts',(16.6170004192108,19.2123322681752,6.31236840866332));
#184654=CARTESIAN_POINT('Ctrl Pts',(16.6169565155957,19.1425685851102,6.30846211078004));
#184655=CARTESIAN_POINT('Ctrl Pts',(16.6203610680012,19.0728499211983,6.30447846496045));
#184656=CARTESIAN_POINT('Ctrl Pts',(16.6282130558034,18.9931538165595,6.29977938873572));
#184657=CARTESIAN_POINT('Ctrl Pts',(16.6293006053898,18.9828858472482,6.29917122396499));
#184658=CARTESIAN_POINT('Ctrl Pts',(16.6312636169845,18.9655631792681,6.29814040880299));
#184659=CARTESIAN_POINT('Ctrl Pts',(16.6320995838046,18.9585041228973,6.29771899770064));
#184660=CARTESIAN_POINT('Ctrl Pts',(16.6337050914328,18.9455077401542,6.29694059639473));
#184661=CARTESIAN_POINT('Ctrl Pts',(16.634464299231,18.9395691928747,6.29658393470745));
#184662=CARTESIAN_POINT('Ctrl Pts',(16.6360836208655,18.9273162371326,6.29584597873218));
#184663=CARTESIAN_POINT('Ctrl Pts',(16.6369470759956,18.9210023384499,6.29546458234972));
#184664=CARTESIAN_POINT('Ctrl Pts',(16.6389493188803,18.9068379206268,6.29460638823001));
#184665=CARTESIAN_POINT('Ctrl Pts',(16.6401037459456,18.8989897412374,6.29412909998424));
#184666=CARTESIAN_POINT('Ctrl Pts',(16.6431530579818,18.8790389677552,6.29291117245185));
#184667=CARTESIAN_POINT('Ctrl Pts',(16.6451089122256,18.8669461155635,6.29216861091687));
#184668=CARTESIAN_POINT('Ctrl Pts',(16.6571576857211,18.7963431733557,6.28780731602315));
#184669=CARTESIAN_POINT('Ctrl Pts',(16.669602709355,18.7382664482567,6.28411436415114));
#184670=CARTESIAN_POINT('Ctrl Pts',(16.6998137463031,18.621484745341,6.27646813719084));
#184671=CARTESIAN_POINT('Ctrl Pts',(16.717722832186,18.5628739506456,6.27251385443586));
#184672=CARTESIAN_POINT('Ctrl Pts',(16.7924559939099,18.3515665971345,6.25787329615711));
#184673=CARTESIAN_POINT('Ctrl Pts',(16.8643036033861,18.2047920773384,6.24690410269838));
#184674=CARTESIAN_POINT('Ctrl Pts',(16.9697240495311,18.0405025951793,6.23450257797181));
#184675=CARTESIAN_POINT('Ctrl Pts',(16.987802329498,18.0136998020795,6.23247694995395));
#184676=CARTESIAN_POINT('Ctrl Pts',(17.0106658357274,17.9814225980431,6.23004470045211));
#184677=CARTESIAN_POINT('Ctrl Pts',(17.0148734519403,17.9755465834849,6.22960221030077));
#184678=CARTESIAN_POINT('Ctrl Pts',(17.0215192307861,17.9663653220214,6.22891143743443));
#184679=CARTESIAN_POINT('Ctrl Pts',(17.0239370153296,17.9630454913432,6.22866179006326));
#184680=CARTESIAN_POINT('Ctrl Pts',(17.028475893849,17.9568511712821,6.2281962564559));
#184681=CARTESIAN_POINT('Ctrl Pts',(17.0305945790737,17.9539750466186,6.22798021579625));
#184682=CARTESIAN_POINT('Ctrl Pts',(17.0354495871139,17.9474191667884,6.22748801396749));
#184683=CARTESIAN_POINT('Ctrl Pts',(17.038190586786,17.9437429376256,6.22721218338876));
#184684=CARTESIAN_POINT('Ctrl Pts',(17.0466593324388,17.9324613345757,6.22636615020504));
#184685=CARTESIAN_POINT('Ctrl Pts',(17.0524265475302,17.9248855498061,6.2257986358639));
#184686=CARTESIAN_POINT('Ctrl Pts',(17.131399595986,17.8225863412034,6.21813967631868));
#184687=CARTESIAN_POINT('Ctrl Pts',(17.2124720665144,17.7341853090147,6.21156686849477));
#184688=CARTESIAN_POINT('Ctrl Pts',(17.3807398236116,17.579363810668,6.19912101925036));
#184689=CARTESIAN_POINT('Ctrl Pts',(17.4664542438363,17.5119189009061,6.19325458438613));
#184690=CARTESIAN_POINT('Ctrl Pts',(17.602337401369,17.4210258510781,6.18416056430124));
#184691=CARTESIAN_POINT('Ctrl Pts',(17.6488553017149,17.3924489159956,6.18108186558282));
#184692=CARTESIAN_POINT('Ctrl Pts',(17.7161508456552,17.3546098654913,6.17663925726683));
#184693=CARTESIAN_POINT('Ctrl Pts',(17.7360547168734,17.3438346648476,6.17532671917997));
#184694=CARTESIAN_POINT('Ctrl Pts',(17.7713963088992,17.3254285944372,6.17299628147911));
#184695=CARTESIAN_POINT('Ctrl Pts',(17.7867617135374,17.3176630003485,6.1719831268734));
#184696=CARTESIAN_POINT('Ctrl Pts',(17.8095970250455,17.3064697062356,6.17047677323766));
#184697=CARTESIAN_POINT('Ctrl Pts',(17.8169951643321,17.3028965886442,6.16998864911109));
#184698=CARTESIAN_POINT('Ctrl Pts',(17.8299402229467,17.2967371196819,6.16913429260064));
#184699=CARTESIAN_POINT('Ctrl Pts',(17.8354779406155,17.2941315738855,6.16876873132942));
#184700=CARTESIAN_POINT('Ctrl Pts',(17.8465312432968,17.2889893179297,6.16803887857226));
#184701=CARTESIAN_POINT('Ctrl Pts',(17.8520465971253,17.2864522479085,6.1676746038834));
#184702=CARTESIAN_POINT('Ctrl Pts',(17.8652482178071,17.2804481515462,6.16680241094147));
#184703=CARTESIAN_POINT('Ctrl Pts',(17.8729443910845,17.277003274623,6.16629373687422));
#184704=CARTESIAN_POINT('Ctrl Pts',(17.9007359895117,17.2647622742867,6.16445598627644));
#184705=CARTESIAN_POINT('Ctrl Pts',(17.9209467244247,17.2562328756557,6.1631178586342));
#184706=CARTESIAN_POINT('Ctrl Pts',(18.1149099096541,17.1779043529848,6.15025580521359));
#184707=CARTESIAN_POINT('Ctrl Pts',(18.2970384827337,17.1311474235341,6.13791611220657));
#184708=CARTESIAN_POINT('Ctrl Pts',(18.590169829228,17.0961299255959,6.11842865333243));
#184709=CARTESIAN_POINT('Ctrl Pts',(18.6982876997502,17.0915443065402,6.11134587412142));
#184710=CARTESIAN_POINT('Ctrl Pts',(18.818076798322,17.0956373579118,6.10391453086623));
#184711=CARTESIAN_POINT('Ctrl Pts',(18.8298571490593,17.0961384354843,6.1031882747177));
#184712=CARTESIAN_POINT('Ctrl Pts',(18.8466289590057,17.0969922559585,6.10216137923623));
#184713=CARTESIAN_POINT('Ctrl Pts',(18.8516240580739,17.0972643007188,6.10185643752921));
#184714=CARTESIAN_POINT('Ctrl Pts',(18.8602421026819,17.0977643036436,6.10133192220937));
#184715=CARTESIAN_POINT('Ctrl Pts',(18.8638654965303,17.0979838783303,6.10111188277366));
#184716=CARTESIAN_POINT('Ctrl Pts',(18.8708989996912,17.098428263302,6.10068572536461));
#184717=CARTESIAN_POINT('Ctrl Pts',(18.8743091279023,17.0986520107185,6.10047954649683));
#184718=CARTESIAN_POINT('Ctrl Pts',(18.8835278942027,17.0992793007773,6.09992332590626));
#184719=CARTESIAN_POINT('Ctrl Pts',(18.8893354836968,17.0996985549199,6.09957415889668));
#184720=CARTESIAN_POINT('Ctrl Pts',(18.9109978308911,17.1013522423937,6.09827613890788));
#184721=CARTESIAN_POINT('Ctrl Pts',(18.9268407033244,17.1027413843944,6.0973355741368));
#184722=CARTESIAN_POINT('Ctrl Pts',(19.0615894733413,17.1160881985625,6.08939895648375));
#184723=CARTESIAN_POINT('Ctrl Pts',(19.1793174165336,17.1379177183873,6.08287716869521));
#184724=CARTESIAN_POINT('Ctrl Pts',(19.3146076221558,17.1750690365644,6.07525157666226));
#184725=CARTESIAN_POINT('Ctrl Pts',(19.3345474168016,17.1808613591687,6.0741244965783));
#184726=CARTESIAN_POINT('Ctrl Pts',(19.4981736546786,17.2310149241983,6.0648296390241));
#184727=CARTESIAN_POINT('Ctrl Pts',(19.6368246428032,17.2902702806385,6.05661875674878));
#184728=CARTESIAN_POINT('Ctrl Pts',(19.7866497988288,17.3741349812198,6.04662022869469));
#184729=CARTESIAN_POINT('Ctrl Pts',(19.8051179017931,17.3848425348311,6.0453676051467));
#184730=CARTESIAN_POINT('Ctrl Pts',(19.8311392445454,17.4004598819164,6.04357238647367));
#184731=CARTESIAN_POINT('Ctrl Pts',(19.8388283240229,17.4051416412863,6.04303809467623));
#184732=CARTESIAN_POINT('Ctrl Pts',(19.8520386863013,17.413301173094,6.04211342597836));
#184733=CARTESIAN_POINT('Ctrl Pts',(19.8575742217757,17.4167557181318,6.04172390769436));
#184734=CARTESIAN_POINT('Ctrl Pts',(19.8681406098919,17.4234179249885,6.04097640017878));
#184735=CARTESIAN_POINT('Ctrl Pts',(19.873174053312,17.4266213762106,6.04061856970972));
#184736=CARTESIAN_POINT('Ctrl Pts',(19.8862234551213,17.4350041693775,6.03968629443089));
#184737=CARTESIAN_POINT('Ctrl Pts',(19.894217985573,17.4402164722338,6.03911062305968));
#184738=CARTESIAN_POINT('Ctrl Pts',(19.9213380639449,17.4581608146675,6.03714209289007));
#184739=CARTESIAN_POINT('Ctrl Pts',(19.9402909418736,17.4711497231062,6.03573960073047));
#184740=CARTESIAN_POINT('Ctrl Pts',(20.1023489603674,17.5861333331857,6.02350908742361));
#184741=CARTESIAN_POINT('Ctrl Pts',(20.232424736463,17.7052542249308,6.01197518188425));
#184742=CARTESIAN_POINT('Ctrl Pts',(20.4025476063424,17.9051747710723,5.99463124731251));
#184743=CARTESIAN_POINT('Ctrl Pts',(20.4547084097663,17.9747172150472,5.98890822571665));
#184744=CARTESIAN_POINT('Ctrl Pts',(20.5232203794133,18.078830946225,5.98095120531324));
#184745=CARTESIAN_POINT('Ctrl Pts',(20.5431413093442,18.1109434268952,5.97857480656709));
#184746=CARTESIAN_POINT('Ctrl Pts',(20.5660099146122,18.1501107659587,5.97578388234448));
#184747=CARTESIAN_POINT('Ctrl Pts',(20.5697914552091,18.1566679692348,5.97532018129335));
#184748=CARTESIAN_POINT('Ctrl Pts',(20.575607443078,18.1668790719648,5.97460374172046));
#184749=CARTESIAN_POINT('Ctrl Pts',(20.5776663262049,18.1705188780772,5.97434947037159));
#184750=CARTESIAN_POINT('Ctrl Pts',(20.5814598464087,18.1772718846935,5.97387979824542));
#184751=CARTESIAN_POINT('Ctrl Pts',(20.5831973923774,18.1803833376125,5.97366421551522));
#184752=CARTESIAN_POINT('Ctrl Pts',(20.5871018201758,18.1874167253598,5.97317872850792));
#184753=CARTESIAN_POINT('Ctrl Pts',(20.5892641066467,18.191341149453,5.97290911947326));
#184754=CARTESIAN_POINT('Ctrl Pts',(20.5955921278758,18.2029129088761,5.9721178050488));
#184755=CARTESIAN_POINT('Ctrl Pts',(20.5997232136719,18.210579223666,5.97159825710449));
#184756=CARTESIAN_POINT('Ctrl Pts',(20.6287270562532,18.2652080140096,5.96792775935897));
#184757=CARTESIAN_POINT('Ctrl Pts',(20.651873235906,18.3130710726034,5.96487741648899));
#184758=CARTESIAN_POINT('Ctrl Pts',(20.6798121033316,18.376867917237,5.96095996447022));
#184759=CARTESIAN_POINT('Ctrl Pts',(20.6862522894806,18.39205428076,5.96003817743331));
#184760=CARTESIAN_POINT('Ctrl Pts',(20.7491920882494,18.5454333388108,5.95082138560431));
#184761=CARTESIAN_POINT('Ctrl Pts',(20.791101642102,18.6891623393364,5.94290867633278));
#184762=CARTESIAN_POINT('Ctrl Pts',(20.8284515169959,18.8967433226113,5.93123900740156));
#184763=CARTESIAN_POINT('Ctrl Pts',(20.8367085905795,18.9578199314932,5.92778147937456));
#184764=CARTESIAN_POINT('Ctrl Pts',(20.8456588766408,19.0561854772819,5.92211276298996));
#184765=CARTESIAN_POINT('Ctrl Pts',(20.8480514786509,19.0932848975868,5.91995236629277));
#184766=CARTESIAN_POINT('Ctrl Pts',(20.8498895661266,19.1415440858307,5.91710550848403));
#184767=CARTESIAN_POINT('Ctrl Pts',(20.8502253572454,19.1526646739699,5.91644698714222));
#184768=CARTESIAN_POINT('Ctrl Pts',(20.8506288686729,19.1707534518912,5.91537156434363));
#184769=CARTESIAN_POINT('Ctrl Pts',(20.8507498704511,19.1777203290985,5.91495633670887));
#184770=CARTESIAN_POINT('Ctrl Pts',(20.8509164123178,19.191118653724,5.91415576367178));
#184771=CARTESIAN_POINT('Ctrl Pts',(20.8509670427109,19.1975499691306,5.91377058237927));
#184772=CARTESIAN_POINT('Ctrl Pts',(20.8510158622436,19.2122751004777,5.9128865711026));
#184773=CARTESIAN_POINT('Ctrl Pts',(20.8509946200193,19.2205688361206,5.91238713746858));
#184774=CARTESIAN_POINT('Ctrl Pts',(20.8508087241339,19.242600213201,5.91105630173106));
#184775=CARTESIAN_POINT('Ctrl Pts',(20.8505590777554,19.2563365685638,5.91022225283596));
#184776=CARTESIAN_POINT('Ctrl Pts',(20.8476398587416,19.3609185330852,5.90383860603307));
#184777=CARTESIAN_POINT('Ctrl Pts',(20.8392567239194,19.4514981272216,5.8981102386584));
#184778=CARTESIAN_POINT('Ctrl Pts',(20.8031448642124,19.6801521332451,5.88315996263288));
#184779=CARTESIAN_POINT('Ctrl Pts',(20.767422157897,19.816519274104,5.87376079530364));
#184780=CARTESIAN_POINT('Ctrl Pts',(20.6996340287677,19.9989661971492,5.86102203016596));
#184781=CARTESIAN_POINT('Ctrl Pts',(20.6788842038614,20.0488747471659,5.85752348186857));
#184782=CARTESIAN_POINT('Ctrl Pts',(20.6444950821597,20.1234057475967,5.85233052105096));
#184783=CARTESIAN_POINT('Ctrl Pts',(20.632238314744,20.1486391548369,5.85057818432761));
#184784=CARTESIAN_POINT('Ctrl Pts',(20.6163414822344,20.1797761746192,5.84842992567003));
#184785=CARTESIAN_POINT('Ctrl Pts',(20.6131697982816,20.1859141523834,5.84800713607432));
#184786=CARTESIAN_POINT('Ctrl Pts',(20.608097485461,20.1956135835784,5.8473402619125));
#184787=CARTESIAN_POINT('Ctrl Pts',(20.6062166535164,20.1991852543446,5.8470949615153));
#184788=CARTESIAN_POINT('Ctrl Pts',(20.602646121178,20.2059188540867,5.84663303630614));
#184789=CARTESIAN_POINT('Ctrl Pts',(20.6009586259146,20.2090818311675,5.84641628365501));
#184790=CARTESIAN_POINT('Ctrl Pts',(20.5970768855037,20.2163133269775,5.84592122358843));
#184791=CARTESIAN_POINT('Ctrl Pts',(20.5948773467003,20.2203789517136,5.84564325642433));
#184792=CARTESIAN_POINT('Ctrl Pts',(20.588991542109,20.2311736353698,5.8449060971944));
#184793=CARTESIAN_POINT('Ctrl Pts',(20.5852819423108,20.237889985202,5.84444835095195));
#184794=CARTESIAN_POINT('Ctrl Pts',(20.5587289344699,20.2853535029882,5.84121890670733));
#184795=CARTESIAN_POINT('Ctrl Pts',(20.5345770239711,20.3253582120293,5.83852513941421));
#184796=CARTESIAN_POINT('Ctrl Pts',(20.5066902352816,20.3682718787163,5.83563022696328));
#184797=CARTESIAN_POINT('Ctrl Pts',(20.5042494338873,20.3720020731314,5.83537854795465));
#184798=CARTESIAN_POINT('Ctrl Pts',(20.488964655291,20.3952010204539,5.83381284591427));
#184799=CARTESIAN_POINT('Ctrl Pts',(20.475811128374,20.4144646014065,5.83251074399911));
#184800=CARTESIAN_POINT('Ctrl Pts',(20.436063257422,20.4706588647084,5.82869455095512));
#184801=CARTESIAN_POINT('Ctrl Pts',(20.4085930680496,20.5069545043392,5.82620629270073));
#184802=CARTESIAN_POINT('Ctrl Pts',(20.311206949939,20.6273559769229,5.81777526116459));
#184803=CARTESIAN_POINT('Ctrl Pts',(20.2359570160179,20.7069178635393,5.81188725091448));
#184804=CARTESIAN_POINT('Ctrl Pts',(20.1140504702378,20.8172959257157,5.80274310063257));
#184805=CARTESIAN_POINT('Ctrl Pts',(20.0717733010439,20.8526722727376,5.79963569084847));
#184806=CARTESIAN_POINT('Ctrl Pts',(20.0010165702779,20.9073298510568,5.79449184046196));
#184807=CARTESIAN_POINT('Ctrl Pts',(19.973362244009,20.9276382800376,5.79249478428642));
#184808=CARTESIAN_POINT('Ctrl Pts',(19.936362907771,20.9534492154566,5.78983420080694));
#184809=CARTESIAN_POINT('Ctrl Pts',(19.9274509174513,20.959565335212,5.78919420039052));
#184810=CARTESIAN_POINT('Ctrl Pts',(19.912775274409,20.9694724726168,5.78814150080957));
#184811=CARTESIAN_POINT('Ctrl Pts',(19.9070391670171,20.9733040871034,5.78773034288755));
#184812=CARTESIAN_POINT('Ctrl Pts',(19.8958978650463,20.9806677773008,5.78693227511242));
#184813=CARTESIAN_POINT('Ctrl Pts',(19.8904950303831,20.9842032974486,5.78654550062686));
#184814=CARTESIAN_POINT('Ctrl Pts',(19.877980389055,20.9923111330704,5.78565011693736));
#184815=CARTESIAN_POINT('Ctrl Pts',(19.8708572321126,20.9968656483333,5.78514085158098));
#184816=CARTESIAN_POINT('Ctrl Pts',(19.8516216677252,21.0090030635592,5.78376652196445));
#184817=CARTESIAN_POINT('Ctrl Pts',(19.8394596093548,21.016506091129,5.78289852949736));
#184818=CARTESIAN_POINT('Ctrl Pts',(19.7271457923959,21.0842346020385,5.7748902304401));
#184819=CARTESIAN_POINT('Ctrl Pts',(19.622260152372,21.1361837654899,5.76744805632574));
#184820=CARTESIAN_POINT('Ctrl Pts',(19.3623099480332,21.2391542491379,5.7491845267281));
#184821=CARTESIAN_POINT('Ctrl Pts',(19.2045759373841,21.2814447388487,5.7382229964832));
#184822=CARTESIAN_POINT('Ctrl Pts',(19.0114506289459,21.3099910378608,5.72581868878594));
#184823=CARTESIAN_POINT('Ctrl Pts',(18.979238999151,21.3139979384514,5.72378472573837));
#184824=CARTESIAN_POINT('Ctrl Pts',(18.9397468188438,21.3179906513314,5.72134388173058));
#184825=CARTESIAN_POINT('Ctrl Pts',(18.9325438129288,21.3186815974175,5.72090083859543));
#184826=CARTESIAN_POINT('Ctrl Pts',(18.9212452494466,21.3197069733,5.72020939567705));
#184827=CARTESIAN_POINT('Ctrl Pts',(18.9171520988964,21.3200664266488,5.71995962695819));
#184828=CARTESIAN_POINT('Ctrl Pts',(18.9094986848361,21.3207160877295,5.7194939883818));
#184829=CARTESIAN_POINT('Ctrl Pts',(18.9059387726566,21.3210091985323,5.71927796336941));
#184830=CARTESIAN_POINT('Ctrl Pts',(18.8978100015833,21.3216577845141,5.71878595431076));
#184831=CARTESIAN_POINT('Ctrl Pts',(18.8932407284774,21.3220074351477,5.71851029985663));
#184832=CARTESIAN_POINT('Ctrl Pts',(18.8791899587085,21.3230367504431,5.71766534360018));
#184833=CARTESIAN_POINT('Ctrl Pts',(18.8697048403569,21.323667404789,5.71709872014334));
#184834=CARTESIAN_POINT('Ctrl Pts',(18.7843133952374,21.3287675174094,5.71202896160059));
#184835=CARTESIAN_POINT('Ctrl Pts',(18.7082130956363,21.3292087594809,5.70773301599004));
#184836=CARTESIAN_POINT('Ctrl Pts',(18.5898217065979,21.3235116889203,5.7011734030744));
#184837=CARTESIAN_POINT('Ctrl Pts',(18.5474670245872,21.3201938382711,5.69885162815144));
#184838=CARTESIAN_POINT('Ctrl Pts',(18.3965610211972,21.3037910967691,5.69058743402106));
#184839=CARTESIAN_POINT('Ctrl Pts',(18.2889614934931,21.2835779791375,5.68470085103502));
#184840=CARTESIAN_POINT('Ctrl Pts',(18.130230761718,21.2408238184274,5.67556001884216));
#184841=CARTESIAN_POINT('Ctrl Pts',(18.0776354941847,21.2244316522273,5.67245451086984));
#184842=CARTESIAN_POINT('Ctrl Pts',(17.993426801835,21.1945362864908,5.66731352801543));
#184843=CARTESIAN_POINT('Ctrl Pts',(17.9613969313275,21.1822810970606,5.66531738000108));
#184844=CARTESIAN_POINT('Ctrl Pts',(17.9196834756504,21.1651479956976,5.66265783498603));
#184845=CARTESIAN_POINT('Ctrl Pts',(17.9097185978435,21.1609656290359,5.66201794143761));
#184846=CARTESIAN_POINT('Ctrl Pts',(17.8934466836655,21.1539891150937,5.66096537286275));
#184847=CARTESIAN_POINT('Ctrl Pts',(17.8871204308637,21.1512400811811,5.66055423832578));
#184848=CARTESIAN_POINT('Ctrl Pts',(17.8748983878731,21.1458579051056,5.65975618393457));
#184849=CARTESIAN_POINT('Ctrl Pts',(17.8690009810089,21.1432286067182,5.65936939927833));
#184850=CARTESIAN_POINT('Ctrl Pts',(17.8554086028623,21.1370938858025,5.65847394540759));
#184851=CARTESIAN_POINT('Ctrl Pts',(17.8477224594032,21.133569275174,5.65796461971706));
#184852=CARTESIAN_POINT('Ctrl Pts',(17.8271010186974,21.1239630273187,5.65659002170384));
#184853=CARTESIAN_POINT('Ctrl Pts',(17.8142060312325,21.1177963565797,5.6557218193945));
#184854=CARTESIAN_POINT('Ctrl Pts',(17.6962263657607,21.0599006259921,5.64769730628469));
#184855=CARTESIAN_POINT('Ctrl Pts',(17.5955588308435,20.9996731073894,5.64023770815659));
#184856=CARTESIAN_POINT('Ctrl Pts',(17.3674344252407,20.8361021302941,5.62190024360743));
#184857=CARTESIAN_POINT('Ctrl Pts',(17.2459727671715,20.7256727598796,5.61087998248642));
#184858=CARTESIAN_POINT('Ctrl Pts',(17.1177578696254,20.578640553775,5.59849615577485));
#184859=CARTESIAN_POINT('Ctrl Pts',(17.0976054600739,20.554462862586,5.59652524617231));
#184860=CARTESIAN_POINT('Ctrl Pts',(17.073533384635,20.5242368367764,5.59414951220226));
#184861=CARTESIAN_POINT('Ctrl Pts',(17.069096744174,20.5186075566984,5.59371071827025));
#184862=CARTESIAN_POINT('Ctrl Pts',(17.0621710466282,20.509727727231,5.59302442527478));
#184863=CARTESIAN_POINT('Ctrl Pts',(17.0596627311824,20.5064923657495,5.59277559001715));
#184864=CARTESIAN_POINT('Ctrl Pts',(17.0549819932017,20.5004185931482,5.59231075336545));
#184865=CARTESIAN_POINT('Ctrl Pts',(17.0528073988883,20.4975819887177,5.59209460245688));
#184866=CARTESIAN_POINT('Ctrl Pts',(17.04784704518,20.4910775077477,5.59160108525473));
#184867=CARTESIAN_POINT('Ctrl Pts',(17.0450660695357,20.4874060452441,5.59132405634155));
#184868=CARTESIAN_POINT('Ctrl Pts',(17.0378180163142,20.4777719545303,5.59060104906631));
#184869=CARTESIAN_POINT('Ctrl Pts',(17.0333703493831,20.4717947103745,5.59015639466206));
#184870=CARTESIAN_POINT('Ctrl Pts',(17.0039154534772,20.431770655083,5.58720407347442));
#184871=CARTESIAN_POINT('Ctrl Pts',(16.9798987171932,20.3970028494053,5.58476001380223));
#184872=CARTESIAN_POINT('Ctrl Pts',(16.9164818751446,20.2990523040206,5.578131728505));
#184873=CARTESIAN_POINT('Ctrl Pts',(16.8793478434617,20.2344729185197,5.57404407031446));
#184874=CARTESIAN_POINT('Ctrl Pts',(16.8077027734305,20.0931161146977,5.56540886713027));
#184875=CARTESIAN_POINT('Ctrl Pts',(16.7742226496541,20.015993096988,5.5608776586747));
#184876=CARTESIAN_POINT('Ctrl Pts',(16.7454193397875,19.9371101554369,5.55626850699162));
#184877=CARTESIAN_POINT('',(16.6170004656572,19.212404133962,6.08905627902251));
#184878=CARTESIAN_POINT('Ctrl Pts',(16.7454193775548,19.9371102588694,5.3354009189409));
#184879=CARTESIAN_POINT('Ctrl Pts',(16.7544339441791,19.961798234683,5.33706788906197));
#184880=CARTESIAN_POINT('Ctrl Pts',(16.7639100391653,19.9863232181294,5.3387164058795));
#184881=CARTESIAN_POINT('Ctrl Pts',(16.777502883358,20.0196419980515,5.34093968445625));
#184882=CARTESIAN_POINT('Ctrl Pts',(16.7812238464107,20.0285867847519,5.34153491310857));
#184883=CARTESIAN_POINT('Ctrl Pts',(16.7868091135218,20.0417574724739,5.34240859485602));
#184884=CARTESIAN_POINT('Ctrl Pts',(16.7886259932689,20.0460031744388,5.34268980911402));
#184885=CARTESIAN_POINT('Ctrl Pts',(16.7918742109988,20.0535254915758,5.34318724929614));
#184886=CARTESIAN_POINT('Ctrl Pts',(16.7932999700288,20.0568044564834,5.34340380962984));
#184887=CARTESIAN_POINT('Ctrl Pts',(16.7963728336328,20.0638227594099,5.34386674048004));
#184888=CARTESIAN_POINT('Ctrl Pts',(16.7980224537958,20.0675609354005,5.34411295448142));
#184889=CARTESIAN_POINT('Ctrl Pts',(16.8025810914609,20.0778107421036,5.34478713350902));
#184890=CARTESIAN_POINT('Ctrl Pts',(16.8055122380113,20.0843125546128,5.34521376469351));
#184891=CARTESIAN_POINT('Ctrl Pts',(16.8213484052609,20.1189714913306,5.34748314907788));
#184892=CARTESIAN_POINT('Ctrl Pts',(16.834838068308,20.1468592507548,5.34929205620498));
#184893=CARTESIAN_POINT('Ctrl Pts',(16.923351945796,20.3200448294343,5.36047870403886));
#184894=CARTESIAN_POINT('Ctrl Pts',(17.0143947027808,20.4565507925658,5.36912122011465));
#184895=CARTESIAN_POINT('Ctrl Pts',(17.1964660742112,20.6709803088658,5.38451635931984));
#184896=CARTESIAN_POINT('Ctrl Pts',(17.2800215755344,20.754209145727,5.3910866106989));
#184897=CARTESIAN_POINT('Ctrl Pts',(17.3809923330283,20.8392701814967,5.39882093310458));
#184898=CARTESIAN_POINT('Ctrl Pts',(17.3920227743076,20.8483730917581,5.39966311054418));
#184899=CARTESIAN_POINT('Ctrl Pts',(17.4097221163544,20.8626805458267,5.40101056154017));
#184900=CARTESIAN_POINT('Ctrl Pts',(17.4163315624945,20.8679581842069,5.40151288786934));
#184901=CARTESIAN_POINT('Ctrl Pts',(17.4280424976804,20.8771949765441,5.40240152827851));
#184902=CARTESIAN_POINT('Ctrl Pts',(17.4331308360002,20.8811706842279,5.40278717523398));
#184903=CARTESIAN_POINT('Ctrl Pts',(17.4436912486585,20.8893443902878,5.40358664064369));
#184904=CARTESIAN_POINT('Ctrl Pts',(17.4491658013981,20.893539047556,5.40400058488819));
#184905=CARTESIAN_POINT('Ctrl Pts',(17.463267746161,20.9042351398811,5.40506564150212));
#184906=CARTESIAN_POINT('Ctrl Pts',(17.4719245040262,20.9106973658753,5.40571828086096));
#184907=CARTESIAN_POINT('Ctrl Pts',(17.5082358078944,20.9373732223715,5.40845127515022));
#184908=CARTESIAN_POINT('Ctrl Pts',(17.5363281845071,20.9569794857325,5.41055489606549));
#184909=CARTESIAN_POINT('Ctrl Pts',(17.6107287427854,21.006264570175,5.41610185071595));
#184910=CARTESIAN_POINT('Ctrl Pts',(17.657737404476,21.0348342039408,5.41958344038907));
#184911=CARTESIAN_POINT('Ctrl Pts',(17.8013463601432,21.1146263085033,5.4301424167401));
#184912=CARTESIAN_POINT('Ctrl Pts',(17.9008522408567,21.1602299190793,5.43736822902282));
#184913=CARTESIAN_POINT('Ctrl Pts',(18.0393905751237,21.2111687889858,5.44711889627765));
#184914=CARTESIAN_POINT('Ctrl Pts',(18.0757096759983,21.223414317916,5.44964642969172));
#184915=CARTESIAN_POINT('Ctrl Pts',(18.1433562209983,21.2441949242656,5.4542826852589));
#184916=CARTESIAN_POINT('Ctrl Pts',(18.1745867685859,21.2530084851222,5.45639558446573));
#184917=CARTESIAN_POINT('Ctrl Pts',(18.2118473304785,21.2626047237027,5.45887544351266));
#184918=CARTESIAN_POINT('Ctrl Pts',(18.2176925584192,21.264083529621,5.45926328100635));
#184919=CARTESIAN_POINT('Ctrl Pts',(18.2659623431375,21.2760763014428,5.4624558313449));
#184920=CARTESIAN_POINT('Ctrl Pts',(18.3087003187832,21.2852999220158,5.46521773804927));
#184921=CARTESIAN_POINT('Ctrl Pts',(18.3590979538321,21.2945532355313,5.46837575808301));
#184922=CARTESIAN_POINT('Ctrl Pts',(18.3665068094078,21.2958727510926,5.46883752280738));
#184923=CARTESIAN_POINT('Ctrl Pts',(18.378483504828,21.297939971009,5.46957979256732));
#184924=CARTESIAN_POINT('Ctrl Pts',(18.3830469602571,21.2987122372992,5.46986163757989));
#184925=CARTESIAN_POINT('Ctrl Pts',(18.3911413482667,21.3000547472274,5.47035977569178));
#184926=CARTESIAN_POINT('Ctrl Pts',(18.3946712274194,21.3006310145012,5.47057640669311));
#184927=CARTESIAN_POINT('Ctrl Pts',(18.4022305204748,21.3018454402684,5.47103902740408));
#184928=CARTESIAN_POINT('Ctrl Pts',(18.406260312497,21.3024808965223,5.47128486300602));
#184929=CARTESIAN_POINT('Ctrl Pts',(18.417311301048,21.3041907984623,5.47195693892841));
#184930=CARTESIAN_POINT('Ctrl Pts',(18.4243361816774,21.3052415748165,5.47238185924092));
#184931=CARTESIAN_POINT('Ctrl Pts',(18.4616276349388,21.3106278588738,5.47462595942983));
#184932=CARTESIAN_POINT('Ctrl Pts',(18.4919818765301,21.3143428866531,5.47641218036499));
#184933=CARTESIAN_POINT('Ctrl Pts',(18.5837084845961,21.3235570210265,5.48171692871855));
#184934=CARTESIAN_POINT('Ctrl Pts',(18.6452535225245,21.3270363587743,5.48515173512579));
#184935=CARTESIAN_POINT('Ctrl Pts',(18.8536821800759,21.3297079786138,5.4966153542393));
#184936=CARTESIAN_POINT('Ctrl Pts',(19.0002920681909,21.3163115321248,5.50442430786287));
#184937=CARTESIAN_POINT('Ctrl Pts',(19.2182167426875,21.2732546711824,5.51682320696274));
#184938=CARTESIAN_POINT('Ctrl Pts',(19.2912573007736,21.2547276470172,5.52111291021559));
#184939=CARTESIAN_POINT('Ctrl Pts',(19.3756992513807,21.22844486701,5.52630186679595));
#184940=CARTESIAN_POINT('Ctrl Pts',(19.3882109231852,21.2244224040183,5.52707667602534));
#184941=CARTESIAN_POINT('Ctrl Pts',(19.4084717195492,21.2176998337835,5.52834142768108));
#184942=CARTESIAN_POINT('Ctrl Pts',(19.4162441413564,21.2150706704276,5.52882903187015));
#184943=CARTESIAN_POINT('Ctrl Pts',(19.4300522611925,21.2103101859927,5.52969968542841));
#184944=CARTESIAN_POINT('Ctrl Pts',(19.4360939776225,21.2081965389819,5.53008214501264));
#184945=CARTESIAN_POINT('Ctrl Pts',(19.4487990135421,21.2036870074794,5.53088963247527));
#184946=CARTESIAN_POINT('Ctrl Pts',(19.4554600727451,21.201285030109,5.53131485938503));
#184947=CARTESIAN_POINT('Ctrl Pts',(19.4730348307368,21.1948477538988,5.53244181401085));
#184948=CARTESIAN_POINT('Ctrl Pts',(19.4839274124168,21.1907558585156,5.53314542521417));
#184949=CARTESIAN_POINT('Ctrl Pts',(19.5342445656523,21.1713789310356,5.53641997972027));
#184950=CARTESIAN_POINT('Ctrl Pts',(19.5732370464033,21.1550055800021,5.53902727968113));
#184951=CARTESIAN_POINT('Ctrl Pts',(19.67913488542,21.1067580669465,5.54630760249952));
#184952=CARTESIAN_POINT('Ctrl Pts',(19.7448932123074,21.072524016115,5.55105562465965));
#184953=CARTESIAN_POINT('Ctrl Pts',(19.9390830510809,20.9581004435283,5.56573480162282));
#184954=CARTESIAN_POINT('Ctrl Pts',(20.0608313137524,20.8675330209865,5.5758983571092));
#184955=CARTESIAN_POINT('Ctrl Pts',(20.1775357144198,20.7595325185273,5.58614714506126));
#184956=CARTESIAN_POINT('Ctrl Pts',(20.1831599882141,20.7542704399681,5.58664232532725));
#184957=CARTESIAN_POINT('Ctrl Pts',(20.2194393197498,20.7199542367006,5.58984406147554));
#184958=CARTESIAN_POINT('Ctrl Pts',(20.2492501853195,20.6900166628813,5.59251041666071));
#184959=CARTESIAN_POINT('Ctrl Pts',(20.2832437881245,20.6537710093413,5.59557253997606));
#184960=CARTESIAN_POINT('Ctrl Pts',(20.2883114837023,20.6483100973081,5.5960296214916));
#184961=CARTESIAN_POINT('Ctrl Pts',(20.2964653202647,20.6394300244387,5.59676584392753));
#184962=CARTESIAN_POINT('Ctrl Pts',(20.2995692646553,20.6360273998208,5.59704629050407));
#184963=CARTESIAN_POINT('Ctrl Pts',(20.3050622913947,20.629966191165,5.59754288331927));
#184964=CARTESIAN_POINT('Ctrl Pts',(20.3074557664947,20.627311662971,5.5977593597154));
#184965=CARTESIAN_POINT('Ctrl Pts',(20.3125762639162,20.6216036787313,5.59822267757644));
#184966=CARTESIAN_POINT('Ctrl Pts',(20.3153011478019,20.6185483792976,5.59846935956072));
#184967=CARTESIAN_POINT('Ctrl Pts',(20.3227724308758,20.6101220597984,5.59914614156427));
#184968=CARTESIAN_POINT('Ctrl Pts',(20.3275004929135,20.6047347515774,5.59957489053217));
#184969=CARTESIAN_POINT('Ctrl Pts',(20.352841915982,20.5755623765655,5.60187605075979));
#184970=CARTESIAN_POINT('Ctrl Pts',(20.3729514447264,20.5513425043393,5.60371348328004));
#184971=CARTESIAN_POINT('Ctrl Pts',(20.4941830292005,20.3985210911496,5.61492681533108));
#184972=CARTESIAN_POINT('Ctrl Pts',(20.5806646642349,20.2589945132311,5.62357181833333));
#184973=CARTESIAN_POINT('Ctrl Pts',(20.7000036850133,20.0048738229282,5.63893985945491));
#184974=CARTESIAN_POINT('Ctrl Pts',(20.740899144624,19.8949273872549,5.64547722215058));
#184975=CARTESIAN_POINT('Ctrl Pts',(20.7763488702799,19.7684086490178,5.65317452707047));
#184976=CARTESIAN_POINT('Ctrl Pts',(20.7800657826988,19.7546065745385,5.65401625584826));
#184977=CARTESIAN_POINT('Ctrl Pts',(20.7857585983334,19.7325813981316,5.65536312304965));
#184978=CARTESIAN_POINT('Ctrl Pts',(20.7878255276099,19.7243821185877,5.65586531828621));
#184979=CARTESIAN_POINT('Ctrl Pts',(20.7913840660744,19.7099002882774,5.65675380597149));
#184980=CARTESIAN_POINT('Ctrl Pts',(20.7928961655522,19.7036228486671,5.65713943203073));
#184981=CARTESIAN_POINT('Ctrl Pts',(20.7959641268665,19.6906253936564,5.65793893186394));
#184982=CARTESIAN_POINT('Ctrl Pts',(20.797515909362,19.6839045028146,5.65835293181163));
#184983=CARTESIAN_POINT('Ctrl Pts',(20.801414550597,19.6666345742438,5.65941829544049));
#184984=CARTESIAN_POINT('Ctrl Pts',(20.8037135071726,19.6560750281829,5.66007118781147));
#184985=CARTESIAN_POINT('Ctrl Pts',(20.8129693057928,19.6119382111154,5.66280663231842));
#184986=CARTESIAN_POINT('Ctrl Pts',(20.8191903550209,19.5782135494089,5.66491250265455));
#184987=CARTESIAN_POINT('Ctrl Pts',(20.8332613485152,19.4899690549339,5.67046680233092));
#184988=CARTESIAN_POINT('Ctrl Pts',(20.8398071948404,19.4352703315242,5.67395361405182));
#184989=CARTESIAN_POINT('Ctrl Pts',(20.8529635413892,19.2713646702355,5.68452262388142));
#184990=CARTESIAN_POINT('Ctrl Pts',(20.8532522858017,19.1618404059941,5.69175321458659));
#184991=CARTESIAN_POINT('Ctrl Pts',(20.8362256226136,18.9346389345337,5.70680369492273));
#184992=CARTESIAN_POINT('Ctrl Pts',(20.8174659751763,18.8174214523578,5.71459553302059));
#184993=CARTESIAN_POINT('Ctrl Pts',(20.7867042156931,18.6931340863944,5.72250388821097));
#184994=CARTESIAN_POINT('Ctrl Pts',(20.7843536763835,18.6839046470247,5.7230889294212));
#184995=CARTESIAN_POINT('Ctrl Pts',(20.7807790666248,18.6702546951491,5.72395055742379));
#184996=CARTESIAN_POINT('Ctrl Pts',(20.7796028246828,18.6658219402288,5.72422979880039));
#184997=CARTESIAN_POINT('Ctrl Pts',(20.7774847484513,18.6579431817837,5.7247250660459));
#184998=CARTESIAN_POINT('Ctrl Pts',(20.7765485891865,18.6544957117868,5.72494141539265));
#184999=CARTESIAN_POINT('Ctrl Pts',(20.7745175056721,18.6470902797724,5.72540536258519));
#185000=CARTESIAN_POINT('Ctrl Pts',(20.7734197935278,18.6431331406509,5.72565279621374));
#185001=CARTESIAN_POINT('Ctrl Pts',(20.7703589450192,18.6322224503572,5.72633376374208));
#185002=CARTESIAN_POINT('Ctrl Pts',(20.768371692712,18.62527564141,5.72676591871478));
#185003=CARTESIAN_POINT('Ctrl Pts',(20.7573066343994,18.5873314203549,5.7291193285026));
#185004=CARTESIAN_POINT('Ctrl Pts',(20.7475553830188,18.5565328807234,5.73100369901553));
#185005=CARTESIAN_POINT('Ctrl Pts',(20.6843962882601,18.3718494027736,5.74221343752147));
#185006=CARTESIAN_POINT('Ctrl Pts',(20.614074331491,18.22431269161,5.75082235854827));
#185007=CARTESIAN_POINT('Ctrl Pts',(20.4654124816059,17.9872492355572,5.76614076296446));
#185008=CARTESIAN_POINT('Ctrl Pts',(20.3952170693221,17.893537402391,5.77266665988033));
#185009=CARTESIAN_POINT('Ctrl Pts',(20.3081689198856,17.7954133933833,5.78035105834047));
#185010=CARTESIAN_POINT('Ctrl Pts',(20.2985772955844,17.7848194011992,5.7811926230152));
#185011=CARTESIAN_POINT('Ctrl Pts',(20.283141441435,17.7681135591141,5.78253927668147));
#185012=CARTESIAN_POINT('Ctrl Pts',(20.2773664779897,17.7619380971408,5.78304142396317));
#185013=CARTESIAN_POINT('Ctrl Pts',(20.2671163535548,17.7511079020324,5.78392985578684));
#185014=CARTESIAN_POINT('Ctrl Pts',(20.2626565749767,17.7464387122417,5.78431547420809));
#185015=CARTESIAN_POINT('Ctrl Pts',(20.2533882466162,17.736823640348,5.78511498666415));
#185016=CARTESIAN_POINT('Ctrl Pts',(20.2485767494453,17.7318807175891,5.78552900701293));
#185017=CARTESIAN_POINT('Ctrl Pts',(20.2361644093598,17.7192534031328,5.78659448307867));
#185018=CARTESIAN_POINT('Ctrl Pts',(20.2285287879964,17.7116036157582,5.7872474681084));
#185019=CARTESIAN_POINT('Ctrl Pts',(20.1964160945631,17.6799203501212,5.78998381047682));
#185020=CARTESIAN_POINT('Ctrl Pts',(20.1714163933101,17.6564262243667,5.79209050516523));
#185021=CARTESIAN_POINT('Ctrl Pts',(20.1048001871039,17.5968029857849,5.79764749742325));
#185022=CARTESIAN_POINT('Ctrl Pts',(20.0623263445061,17.5616748484905,5.80113622378542));
#185023=CARTESIAN_POINT('Ctrl Pts',(19.9315800736052,17.4618694595021,5.81170891158752));
#185024=CARTESIAN_POINT('Ctrl Pts',(19.839618516701,17.4023375356375,5.81894125339262));
#185025=CARTESIAN_POINT('Ctrl Pts',(19.6394028114315,17.2937222205111,5.83398776902141));
#185026=CARTESIAN_POINT('Ctrl Pts',(19.5307617774594,17.2460863805988,5.84177389430751));
#185027=CARTESIAN_POINT('Ctrl Pts',(19.4096763066952,17.2046995755835,5.84967776725404));
#185028=CARTESIAN_POINT('Ctrl Pts',(19.4006354397178,17.2016774617389,5.85026333987533));
#185029=CARTESIAN_POINT('Ctrl Pts',(19.3872134359228,17.1972914176112,5.85112559716426));
#185030=CARTESIAN_POINT('Ctrl Pts',(19.382847927206,17.1958805454932,5.85140494192802));
#185031=CARTESIAN_POINT('Ctrl Pts',(19.3750749252734,17.1933962969234,5.85190032265486));
#185032=CARTESIAN_POINT('Ctrl Pts',(19.3716692737196,17.1923173452727,5.85211668266914));
#185033=CARTESIAN_POINT('Ctrl Pts',(19.364343997581,17.1900169968107,5.85258057481106));
#185034=CARTESIAN_POINT('Ctrl Pts',(19.360423558012,17.1887983826798,5.85282794313175));
#185035=CARTESIAN_POINT('Ctrl Pts',(19.3495984784688,17.1854680585505,5.85350854675179));
#185036=CARTESIAN_POINT('Ctrl Pts',(19.3426864672293,17.1833802327474,5.85394040555768));
#185037=CARTESIAN_POINT('Ctrl Pts',(19.3048667245644,17.1721673129081,5.85628921467593));
#185038=CARTESIAN_POINT('Ctrl Pts',(19.2737625921487,17.1637129799851,5.8581694506292));
#185039=CARTESIAN_POINT('Ctrl Pts',(19.0843022717943,17.1168348102409,5.86937946215354));
#185040=CARTESIAN_POINT('Ctrl Pts',(18.922122912842,17.0960859944393,5.87799152997459));
#185041=CARTESIAN_POINT('Ctrl Pts',(18.6422407799329,17.0927601708337,5.89331429747746));
#185042=CARTESIAN_POINT('Ctrl Pts',(18.5254286145577,17.1010586652293,5.89984123212194));
#185043=CARTESIAN_POINT('Ctrl Pts',(18.3957845772126,17.1211426928271,5.90752679872677));
#185044=CARTESIAN_POINT('Ctrl Pts',(18.3816846858559,17.1234734394357,5.90836837841499));
#185045=CARTESIAN_POINT('Ctrl Pts',(18.3592822518201,17.1274100457792,5.90971505161746));
#185046=CARTESIAN_POINT('Ctrl Pts',(18.3509637133369,17.128923227144,5.91021720328667));
#185047=CARTESIAN_POINT('Ctrl Pts',(18.336308949015,17.1316797939301,5.911105640221));
#185048=CARTESIAN_POINT('Ctrl Pts',(18.3299688934815,17.1329024192921,5.91149125934095));
#185049=CARTESIAN_POINT('Ctrl Pts',(18.3168673866617,17.1354911549738,5.91229077064141));
#185050=CARTESIAN_POINT('Ctrl Pts',(18.3101068282682,17.1368613450159,5.9127047891231));
#185051=CARTESIAN_POINT('Ctrl Pts',(18.2927708556483,17.1404631949202,5.91377025489896));
#185052=CARTESIAN_POINT('Ctrl Pts',(18.2822057128759,17.142742826834,5.91442323144883));
#185053=CARTESIAN_POINT('Ctrl Pts',(18.2381844175133,17.1525946576822,5.91715949163572));
#185054=CARTESIAN_POINT('Ctrl Pts',(18.2048988724773,17.1608981913747,5.91926611086932));
#185055=CARTESIAN_POINT('Ctrl Pts',(18.1187107604473,17.184637739353,5.92482285665088));
#185056=CARTESIAN_POINT('Ctrl Pts',(18.0661857487322,17.2013363055365,5.92831140774156));
#185057=CARTESIAN_POINT('Ctrl Pts',(17.818462093011,17.2908761186209,5.94524253761476));
#185058=CARTESIAN_POINT('Ctrl Pts',(17.6341001254976,17.3902054662756,5.95943301121613));
#185059=CARTESIAN_POINT('Ctrl Pts',(17.4635919657424,17.517549995586,5.97284947871786));
#185060=CARTESIAN_POINT('Ctrl Pts',(17.4599738058426,17.5202703503359,5.9731342582316));
#185061=CARTESIAN_POINT('Ctrl Pts',(17.4399959625427,17.5353914637245,5.97470702341874));
#185062=CARTESIAN_POINT('Ctrl Pts',(17.423807913869,17.548018585342,5.97598271335687));
#185063=CARTESIAN_POINT('Ctrl Pts',(17.4027810304423,17.5649178010054,5.97763860875498));
#185064=CARTESIAN_POINT('Ctrl Pts',(17.3977750243699,17.5689788771942,5.97803275318776));
#185065=CARTESIAN_POINT('Ctrl Pts',(17.389744211289,17.5755548475165,5.97866480676073));
#185066=CARTESIAN_POINT('Ctrl Pts',(17.3867077738271,17.5780553805645,5.9789037278657));
#185067=CARTESIAN_POINT('Ctrl Pts',(17.3810359176436,17.5827527942161,5.97934987943894));
#185068=CARTESIAN_POINT('Ctrl Pts',(17.3783988696818,17.5849476186522,5.97955725237127));
#185069=CARTESIAN_POINT('Ctrl Pts',(17.3721624883266,17.5901638960603,5.98004755583311));
#185070=CARTESIAN_POINT('Ctrl Pts',(17.3685678356643,17.5931909600925,5.98033007749987));
#185071=CARTESIAN_POINT('Ctrl Pts',(17.3573349172615,17.6027143308701,5.98121275565799));
#185072=CARTESIAN_POINT('Ctrl Pts',(17.3497325782802,17.6092530606816,5.98180989252141));
#185073=CARTESIAN_POINT('Ctrl Pts',(17.3319067386628,17.624806676322,5.98321024261232));
#185074=CARTESIAN_POINT('Ctrl Pts',(17.3217231600871,17.6338668663948,5.98401038981313));
#185075=CARTESIAN_POINT('Ctrl Pts',(17.2863073361184,17.6659939691311,5.98679657916471));
#185076=CARTESIAN_POINT('Ctrl Pts',(17.2615458444858,17.6895741242838,5.98875091696551));
#185077=CARTESIAN_POINT('Ctrl Pts',(17.1836732667198,17.7674144459385,5.99496003022765));
#185078=CARTESIAN_POINT('Ctrl Pts',(17.1329039396452,17.823936557484,5.99910803434806));
#185079=CARTESIAN_POINT('Ctrl Pts',(16.977365641622,18.0170482054406,6.01259282767885));
#185080=CARTESIAN_POINT('Ctrl Pts',(16.886198618141,18.1636660640111,6.02185804178627));
#185081=CARTESIAN_POINT('Ctrl Pts',(16.8039951984994,18.3407643153645,6.03320082330143));
#185082=CARTESIAN_POINT('Ctrl Pts',(16.7945621927219,18.361994929621,6.03456160905432));
#185083=CARTESIAN_POINT('Ctrl Pts',(16.7817332891331,18.3921986961956,6.03650075907808));
#185084=CARTESIAN_POINT('Ctrl Pts',(16.7780458554875,18.401046751076,6.03706920654468));
#185085=CARTESIAN_POINT('Ctrl Pts',(16.7721580869819,18.4154492489627,6.03799524114108));
#185086=CARTESIAN_POINT('Ctrl Pts',(16.7699209238234,18.4209885630262,6.03835157757218));
#185087=CARTESIAN_POINT('Ctrl Pts',(16.7652917997284,18.4325916797842,6.03909839166055));
#185088=CARTESIAN_POINT('Ctrl Pts',(16.7629043426113,18.4386572012724,6.03948901651778));
#185089=CARTESIAN_POINT('Ctrl Pts',(16.7572996268585,18.4530916780653,6.04041919582516));
#185090=CARTESIAN_POINT('Ctrl Pts',(16.7541074665818,18.4614701861268,6.04095958597292));
#185091=CARTESIAN_POINT('Ctrl Pts',(16.7435701496538,18.4896646874311,6.04277975918914));
#185092=CARTESIAN_POINT('Ctrl Pts',(16.73646869792,18.509569840471,6.04406762519122));
#185093=CARTESIAN_POINT('Ctrl Pts',(16.6996529283538,18.6178595830961,6.05109143770911));
#185094=CARTESIAN_POINT('Ctrl Pts',(16.6755085002152,18.7080165786977,6.05700832119098));
#185095=CARTESIAN_POINT('Ctrl Pts',(16.6304385570914,18.9354384303446,6.0720588793899));
#185096=CARTESIAN_POINT('Ctrl Pts',(16.6169140925405,19.0737188024872,6.08133516956679));
#185097=CARTESIAN_POINT('Ctrl Pts',(16.6170004105532,19.2123184392235,6.09037076723679));
#185098=CARTESIAN_POINT('Ctrl Pts',(16.7454193623258,19.9371102171621,6.13370787675019));
#185099=CARTESIAN_POINT('Ctrl Pts',(16.7204253462621,19.868659704792,6.12932687783769));
#185100=CARTESIAN_POINT('Ctrl Pts',(16.6989958950762,19.7989890746744,6.12494587892519));
#185101=CARTESIAN_POINT('Ctrl Pts',(16.6812266631735,19.7285042295617,6.12056488001268));
#185102=CARTESIAN_POINT('Ctrl Pts',(16.6634283576886,19.6579040588712,6.11617671301702));
#185103=CARTESIAN_POINT('Ctrl Pts',(16.6493023095371,19.5864874879226,6.11178854602136));
#185104=CARTESIAN_POINT('Ctrl Pts',(16.6388927491981,19.514668581907,6.1074003790257));
#185105=CARTESIAN_POINT('Ctrl Pts',(16.6365508783606,19.4985112615104,6.10641315958675));
#185106=CARTESIAN_POINT('Ctrl Pts',(16.6343969009588,19.4823335858048,6.1054259401478));
#185107=CARTESIAN_POINT('Ctrl Pts',(16.6324309574259,19.4661402737595,6.10443872070886));
#185108=CARTESIAN_POINT('Ctrl Pts',(16.6222201199426,19.3820344615431,6.09931124014674));
#185109=CARTESIAN_POINT('Ctrl Pts',(16.6170567766291,19.2973036553198,6.09418375958462));
#185110=CARTESIAN_POINT('Ctrl Pts',(16.6170004656572,19.212404133962,6.08905627902251));
#185111=CARTESIAN_POINT('Origin',(18.734,19.211,0.));
#185112=CARTESIAN_POINT('',(16.7454193167441,19.9371100923286,7.15616136059514));
#185113=CARTESIAN_POINT('',(16.7486737101886,19.9359290495398,6.93361858560548));
#185114=CARTESIAN_POINT('',(16.7454193623258,19.9371102171621,0.));
#185115=CARTESIAN_POINT('Ctrl Pts',(16.7454193167441,19.9371100923285,7.15616136059514));
#185116=CARTESIAN_POINT('Ctrl Pts',(16.72058404148,19.8690943063269,7.15141135633731));
#185117=CARTESIAN_POINT('Ctrl Pts',(16.6992295000541,19.7997804030581,7.14660724357929));
#185118=CARTESIAN_POINT('Ctrl Pts',(16.6631797956417,19.6570555067128,7.13689818809369));
#185119=CARTESIAN_POINT('Ctrl Pts',(16.6487382401048,19.5837556281975,7.13200641828163));
#185120=CARTESIAN_POINT('Ctrl Pts',(16.6333272127491,19.47567679551,7.12505655919908));
#185121=CARTESIAN_POINT('Ctrl Pts',(16.6292914383807,19.4413956454038,7.12289060683243));
#185122=CARTESIAN_POINT('Ctrl Pts',(16.6254128246439,19.3996888120896,7.12031414819974));
#185123=CARTESIAN_POINT('Ctrl Pts',(16.6247685443226,19.3923450135598,7.11986268382579));
#185124=CARTESIAN_POINT('Ctrl Pts',(16.6238224665814,19.3808732058643,7.11916104264327));
#185125=CARTESIAN_POINT('Ctrl Pts',(16.6234943985934,19.3767475059353,7.11890943103365));
#185126=CARTESIAN_POINT('Ctrl Pts',(16.6229060239836,19.3690631386444,7.11844217309981));
#185127=CARTESIAN_POINT('Ctrl Pts',(16.6226426179176,19.3655048114267,7.11822636057523));
#185128=CARTESIAN_POINT('Ctrl Pts',(16.6220645668203,19.3574183333609,7.11773716432519));
#185129=CARTESIAN_POINT('Ctrl Pts',(16.6217554882611,19.3528898367541,7.11746409552394));
#185130=CARTESIAN_POINT('Ctrl Pts',(16.6209918950657,19.341146123027,7.11675816258681));
#185131=CARTESIAN_POINT('Ctrl Pts',(16.6205597664386,19.3339294407798,7.11632652246368));
#185132=CARTESIAN_POINT('Ctrl Pts',(16.6180743367168,19.2885248652664,7.11362363845074));
#185133=CARTESIAN_POINT('Ctrl Pts',(16.6170190194794,19.2502868211829,7.11140439779203));
#185134=CARTESIAN_POINT('Ctrl Pts',(16.6169207094246,19.0499008549758,7.09997624691515));
#185135=CARTESIAN_POINT('Ctrl Pts',(16.6354677186578,18.8882767757765,7.0914146059987));
#185136=CARTESIAN_POINT('Ctrl Pts',(16.697373120192,18.6227424401113,7.07645433449783));
#185137=CARTESIAN_POINT('Ctrl Pts',(16.7308397008735,18.5172852405246,7.07026706865739));
#185138=CARTESIAN_POINT('Ctrl Pts',(16.7777126662261,18.4017842718485,7.06296366851757));
#185139=CARTESIAN_POINT('Ctrl Pts',(16.7831788072558,18.3886941649711,7.06212822733765));
#185140=CARTESIAN_POINT('Ctrl Pts',(16.7921001450349,18.3679193848153,7.06078954377303));
#185141=CARTESIAN_POINT('Ctrl Pts',(16.7954704366286,18.360198554762,7.06028918822827));
#185142=CARTESIAN_POINT('Ctrl Pts',(16.8015031073124,18.3466005629783,7.05940284113164));
#185143=CARTESIAN_POINT('Ctrl Pts',(16.8041464536104,18.3407150380274,7.05901750566348));
#185144=CARTESIAN_POINT('Ctrl Pts',(16.8096767358687,18.3285507197677,7.05821750961661));
#185145=CARTESIAN_POINT('Ctrl Pts',(16.8125675913427,18.3222738024234,7.05780271744179));
#185146=CARTESIAN_POINT('Ctrl Pts',(16.8200827135533,18.306164277913,7.05673299011719));
#185147=CARTESIAN_POINT('Ctrl Pts',(16.824751998384,18.2963530053862,7.05607650203869));
#185148=CARTESIAN_POINT('Ctrl Pts',(16.8446948525917,18.2552665261635,7.05330600340075));
#185149=CARTESIAN_POINT('Ctrl Pts',(16.8606622769423,18.2243359423953,7.05116792072756));
#185150=CARTESIAN_POINT('Ctrl Pts',(16.9043949506372,18.1445129749468,7.04550807459811));
#185151=CARTESIAN_POINT('Ctrl Pts',(16.9333567136985,18.0963107614082,7.04194608537279));
#185152=CARTESIAN_POINT('Ctrl Pts',(17.0332356239815,17.9441467814891,7.03023621556654));
#185153=CARTESIAN_POINT('Ctrl Pts',(17.1115050815964,17.8453418741352,7.02187672784344));
#185154=CARTESIAN_POINT('Ctrl Pts',(17.2668985763519,17.6815216670981,7.00699923935122));
#185155=CARTESIAN_POINT('Ctrl Pts',(17.3407876934438,17.6139230516734,7.00047970527239));
#185156=CARTESIAN_POINT('Ctrl Pts',(17.4267853731384,17.5457754225334,6.99370036427314));
#185157=CARTESIAN_POINT('Ctrl Pts',(17.4344245188285,17.5398068480811,6.99310473240185));
#185158=CARTESIAN_POINT('Ctrl Pts',(17.445764028739,17.5310719002186,6.9922305739691));
#185159=CARTESIAN_POINT('Ctrl Pts',(17.4494327556196,17.5282649246882,6.99194928198737));
#185160=CARTESIAN_POINT('Ctrl Pts',(17.455957562755,17.523306510706,6.99145175585015));
#185161=CARTESIAN_POINT('Ctrl Pts',(17.4588099325777,17.5211502795125,6.99123518685502));
#185162=CARTESIAN_POINT('Ctrl Pts',(17.4649328365295,17.5165460398849,6.99077229448187));
#185163=CARTESIAN_POINT('Ctrl Pts',(17.46820498821,17.5141002748762,6.99052612732118));
#185164=CARTESIAN_POINT('Ctrl Pts',(17.4772061329195,17.5074129058347,6.98985220883767));
#185165=CARTESIAN_POINT('Ctrl Pts',(17.4829495621978,17.5031906965051,6.9894257896391));
#185166=CARTESIAN_POINT('Ctrl Pts',(17.5137221177872,17.48080718736,6.98715955739938));
#185167=CARTESIAN_POINT('Ctrl Pts',(17.5391270012329,17.4631659052984,6.98535347914509));
#185168=CARTESIAN_POINT('Ctrl Pts',(17.6171834293574,17.4114608591055,6.97996800388284));
#185169=CARTESIAN_POINT('Ctrl Pts',(17.670972582829,17.3791718881716,6.97647535634526));
#185170=CARTESIAN_POINT('Ctrl Pts',(17.8443351544451,17.2853166413613,6.96564098423607));
#185171=CARTESIAN_POINT('Ctrl Pts',(17.9683763529019,17.2327227022298,6.95847223548385));
#185172=CARTESIAN_POINT('Ctrl Pts',(18.1354765541806,17.1799600069948,6.94874719054158));
#185173=CARTESIAN_POINT('Ctrl Pts',(18.1747300614653,17.1688024927326,6.94645995771917));
#185174=CARTESIAN_POINT('Ctrl Pts',(18.2613895425818,17.1468561114473,6.9413792172179));
#185175=CARTESIAN_POINT('Ctrl Pts',(18.3088928602563,17.1365521158754,6.93857391154233));
#185176=CARTESIAN_POINT('Ctrl Pts',(18.3691073390532,17.1256460298272,6.93497489479974));
#185177=CARTESIAN_POINT('Ctrl Pts',(18.3815281470229,17.1235107383621,6.9342302503282));
#185178=CARTESIAN_POINT('Ctrl Pts',(18.4012400739608,17.1203029562274,6.93304464393182));
#185179=CARTESIAN_POINT('Ctrl Pts',(18.4085191240394,17.1191573925135,6.9326060047524));
#185180=CARTESIAN_POINT('Ctrl Pts',(18.4220931091327,17.1170937080767,6.93178642830714));
#185181=CARTESIAN_POINT('Ctrl Pts',(18.428386505449,17.1161659114605,6.93140580268591));
#185182=CARTESIAN_POINT('Ctrl Pts',(18.4423736284573,17.1141682478164,6.93055839823835));
#185183=CARTESIAN_POINT('Ctrl Pts',(18.4500692266565,17.1131123359472,6.93009118311778));
#185184=CARTESIAN_POINT('Ctrl Pts',(18.4724466641256,17.1101673135602,6.92872967234074));
#185185=CARTESIAN_POINT('Ctrl Pts',(18.4871424980571,17.1083898411278,6.92783186836276));
#185186=CARTESIAN_POINT('Ctrl Pts',(18.6040636929105,17.0954907892379,6.92065848821028));
#185187=CARTESIAN_POINT('Ctrl Pts',(18.7069423435795,17.0916781480667,6.91415209084858));
#185188=CARTESIAN_POINT('Ctrl Pts',(18.965371521894,17.1009223843318,6.89736582808211));
#185189=CARTESIAN_POINT('Ctrl Pts',(19.1199627036541,17.1236597310998,6.88689546229996));
#185190=CARTESIAN_POINT('Ctrl Pts',(19.3214692027319,17.1764660605136,6.87343959309171));
#185191=CARTESIAN_POINT('Ctrl Pts',(19.3717750386442,17.1916703067092,6.8701018920468));
#185192=CARTESIAN_POINT('Ctrl Pts',(19.429685172763,17.2115534175109,6.86632508261371));
#185193=CARTESIAN_POINT('Ctrl Pts',(19.4378858248511,17.2144256218839,6.86579181222299));
#185194=CARTESIAN_POINT('Ctrl Pts',(19.4502843412951,17.2188539759944,6.864988188491));
#185195=CARTESIAN_POINT('Ctrl Pts',(19.4544952206672,17.2203730443919,6.86471571638991));
#185196=CARTESIAN_POINT('Ctrl Pts',(19.4620494720616,17.2231253398173,6.86422777520277));
#185197=CARTESIAN_POINT('Ctrl Pts',(19.4653945612495,17.2243536563548,6.86401202029746));
#185198=CARTESIAN_POINT('Ctrl Pts',(19.4726614368855,17.2270428947367,6.86354399216831));
#185199=CARTESIAN_POINT('Ctrl Pts',(19.4765819850835,17.2285069962313,6.86329191181828));
#185200=CARTESIAN_POINT('Ctrl Pts',(19.4875952580573,17.2326570804441,6.86258491770412));
#185201=CARTESIAN_POINT('Ctrl Pts',(19.4946780103472,17.2353695971053,6.86213156190185));
#185202=CARTESIAN_POINT('Ctrl Pts',(19.5371985711972,17.2519164726156,6.85941696991385));
#185203=CARTESIAN_POINT('Ctrl Pts',(19.5722751929878,17.2666668704421,6.8572072664197));
#185204=CARTESIAN_POINT('Ctrl Pts',(19.6869985088795,17.3185926140793,6.85001915537283));
#185205=CARTESIAN_POINT('Ctrl Pts',(19.7647320449535,17.3597826245643,6.84521009801362));
#185206=CARTESIAN_POINT('Ctrl Pts',(19.98826417719,17.4966876199193,6.83095043571922));
#185207=CARTESIAN_POINT('Ctrl Pts',(20.1250238703399,17.6056678226495,6.82157748275048));
#185208=CARTESIAN_POINT('Ctrl Pts',(20.2630317362106,17.7466626675632,6.81011395802333));
#185209=CARTESIAN_POINT('Ctrl Pts',(20.2789075541949,17.7634218636427,6.8087616492396));
#185210=CARTESIAN_POINT('Ctrl Pts',(20.3009668510425,17.7874848757765,6.80683253601301));
#185211=CARTESIAN_POINT('Ctrl Pts',(20.3073800916207,17.7945765096935,6.80626550795652));
#185212=CARTESIAN_POINT('Ctrl Pts',(20.3177189800645,17.8061659070707,6.8053411571013));
#185213=CARTESIAN_POINT('Ctrl Pts',(20.3216740757082,17.8106373095968,6.80498507587772));
#185214=CARTESIAN_POINT('Ctrl Pts',(20.3299107168838,17.8200289278672,6.80423828567563));
#185215=CARTESIAN_POINT('Ctrl Pts',(20.3341885365228,17.8249523147171,6.80384742723879));
#185216=CARTESIAN_POINT('Ctrl Pts',(20.3443063993688,17.8367063402064,6.80291575077307));
#185217=CARTESIAN_POINT('Ctrl Pts',(20.3501257979505,17.8435545113228,6.80237408985919));
#185218=CARTESIAN_POINT('Ctrl Pts',(20.3695621301139,17.8667242359223,6.8005451855747));
#185219=CARTESIAN_POINT('Ctrl Pts',(20.3829764661924,17.8832133553978,6.79924975319571));
#185220=CARTESIAN_POINT('Ctrl Pts',(20.4545179737507,17.9739097947823,6.79215508146419));
#185221=CARTESIAN_POINT('Ctrl Pts',(20.5078802888537,18.0517248447993,6.78617079225643));
#185222=CARTESIAN_POINT('Ctrl Pts',(20.6403886364046,18.2756349235806,6.76927211376361));
#185223=CARTESIAN_POINT('Ctrl Pts',(20.7078124104089,18.427873873447,6.75808958983998));
#185224=CARTESIAN_POINT('Ctrl Pts',(20.7691588946154,18.6265503484748,6.74476063580065));
#185225=CARTESIAN_POINT('Ctrl Pts',(20.78035455319,18.6670453071644,6.74210947671535));
#185226=CARTESIAN_POINT('Ctrl Pts',(20.7921063400594,18.7150739865797,6.73906263416479));
#185227=CARTESIAN_POINT('Ctrl Pts',(20.7938359889531,18.7223078472805,6.73860631468141));
#185228=CARTESIAN_POINT('Ctrl Pts',(20.7965740799067,18.7340321366793,6.73787107670368));
#185229=CARTESIAN_POINT('Ctrl Pts',(20.7976060491156,18.7385169286411,6.73759085810142));
#185230=CARTESIAN_POINT('Ctrl Pts',(20.7994134524236,18.7464905350783,6.73709451644182));
#185231=CARTESIAN_POINT('Ctrl Pts',(20.8001946831632,18.7499779784092,6.73687806449015));
#185232=CARTESIAN_POINT('Ctrl Pts',(20.8018523809055,18.7574668593314,6.73641462952675));
#185233=CARTESIAN_POINT('Ctrl Pts',(20.8027260645061,18.7614688558192,6.73616780688422));
#185234=CARTESIAN_POINT('Ctrl Pts',(20.8050988503836,18.7724910698027,6.73549024221721));
#185235=CARTESIAN_POINT('Ctrl Pts',(20.8065738863647,18.77951649065,6.73506085643686));
#185236=CARTESIAN_POINT('Ctrl Pts',(20.814354203185,18.8175338226194,6.73275003662018));
#185237=CARTESIAN_POINT('Ctrl Pts',(20.8200004830739,18.8486583518741,6.73090392956567));
#185238=CARTESIAN_POINT('Ctrl Pts',(20.850512431848,19.0413457455191,6.71969134208865));
#185239=CARTESIAN_POINT('Ctrl Pts',(20.8572960915736,19.2052265383463,6.71105306525506));
#185240=CARTESIAN_POINT('Ctrl Pts',(20.8364523929681,19.4850271143387,6.69569421480608));
#185241=CARTESIAN_POINT('Ctrl Pts',(20.8180853299,19.6008460941183,6.68915892052927));
#185242=CARTESIAN_POINT('Ctrl Pts',(20.7868423677917,19.7284277810049,6.68146394380357));
#185243=CARTESIAN_POINT('Ctrl Pts',(20.7833021722063,19.7422757171445,6.68062224423412));
#185244=CARTESIAN_POINT('Ctrl Pts',(20.7774449147178,19.7642570639177,6.67927541499106));
#185245=CARTESIAN_POINT('Ctrl Pts',(20.7752188370284,19.7724144230931,6.67877322824099));
#185246=CARTESIAN_POINT('Ctrl Pts',(20.7712067843076,19.7867770494357,6.67788475038332));
#185247=CARTESIAN_POINT('Ctrl Pts',(20.7694411670793,19.7929879265233,6.67749912561736));
#185248=CARTESIAN_POINT('Ctrl Pts',(20.7657306844781,19.8058167829792,6.67669962337227));
#185249=CARTESIAN_POINT('Ctrl Pts',(20.7637818348715,19.8124335213782,6.6762856196943));
#185250=CARTESIAN_POINT('Ctrl Pts',(20.7586966832466,19.8293923803066,6.67522023573953));
#185251=CARTESIAN_POINT('Ctrl Pts',(20.7555134893519,19.839720129117,6.67456732666094));
#185252=CARTESIAN_POINT('Ctrl Pts',(20.7419000625379,19.8827159553579,6.67183172095038));
#185253=CARTESIAN_POINT('Ctrl Pts',(20.7307563882289,19.9151510461723,6.66972570268485));
#185254=CARTESIAN_POINT('Ctrl Pts',(20.6996742824258,19.9989385344372,6.66417092004486));
#185255=CARTESIAN_POINT('Ctrl Pts',(20.6785117211371,20.0498062143585,6.66068376497394));
#185256=CARTESIAN_POINT('Ctrl Pts',(20.6094732749493,20.1990543145289,6.65011409545868));
#185257=CARTESIAN_POINT('Ctrl Pts',(20.5559344351494,20.2946063773585,6.64288319061463));
#185258=CARTESIAN_POINT('Ctrl Pts',(20.4696794884061,20.4239432277173,6.63261385179871));
#185259=CARTESIAN_POINT('Ctrl Pts',(20.44285269472,20.4614548073539,6.62957403903283));
#185260=CARTESIAN_POINT('Ctrl Pts',(20.4015499634587,20.5153936039311,6.62513734810568));
#185261=CARTESIAN_POINT('Ctrl Pts',(20.3880103889407,20.5325200466475,6.62371844666039));
#185262=CARTESIAN_POINT('Ctrl Pts',(20.3415173540985,20.5894957558536,6.61897087062038));
#185263=CARTESIAN_POINT('Ctrl Pts',(20.3073668783397,20.628349714408,6.61568714388755));
#185264=CARTESIAN_POINT('Ctrl Pts',(20.2658807413723,20.672199917883,6.61196387318168));
#185265=CARTESIAN_POINT('Ctrl Pts',(20.2598980920147,20.6784463616942,6.61143307505074));
#185266=CARTESIAN_POINT('Ctrl Pts',(20.2507671154801,20.6878637307102,6.61063243109202));
#185267=CARTESIAN_POINT('Ctrl Pts',(20.2476468387929,20.6910615561349,6.6103604894806));
#185268=CARTESIAN_POINT('Ctrl Pts',(20.242020096377,20.6967917362461,6.60987311294294));
#185269=CARTESIAN_POINT('Ctrl Pts',(20.2395173531268,20.6993276502774,6.60965739516212));
#185270=CARTESIAN_POINT('Ctrl Pts',(20.2340562560055,20.7048332567298,6.60918900400131));
#185271=CARTESIAN_POINT('Ctrl Pts',(20.231095490396,20.7078004754904,6.60893652590478));
#185272=CARTESIAN_POINT('Ctrl Pts',(20.2227310420603,20.7161335074382,6.60822729039273));
#185273=CARTESIAN_POINT('Ctrl Pts',(20.2173071287359,20.7214790487259,6.60777210682142));
#185274=CARTESIAN_POINT('Ctrl Pts',(20.1842213334862,20.7537366946136,6.60502308558937));
#185275=CARTESIAN_POINT('Ctrl Pts',(20.1558547321966,20.7799193631107,6.60278231242563));
#185276=CARTESIAN_POINT('Ctrl Pts',(20.0589354533622,20.864587669963,6.59544042493736));
#185277=CARTESIAN_POINT('Ctrl Pts',(19.9873644081435,20.9194748687773,6.5905170281054));
#185278=CARTESIAN_POINT('Ctrl Pts',(19.770353960458,21.0648991689962,6.57631228003958));
#185279=CARTESIAN_POINT('Ctrl Pts',(19.6171923558013,21.1425631124966,6.56709194761994));
#185280=CARTESIAN_POINT('Ctrl Pts',(19.4344703438857,21.2088920312135,6.55579964131705));
#185281=CARTESIAN_POINT('Ctrl Pts',(19.412452264007,21.2164759368467,6.55443564420814));
#185282=CARTESIAN_POINT('Ctrl Pts',(19.3811920168881,21.2266695055422,6.55249268978683));
#185283=CARTESIAN_POINT('Ctrl Pts',(19.3720498497566,21.2295820386886,6.55192370271024));
#185284=CARTESIAN_POINT('Ctrl Pts',(19.3571823527064,21.2342074694699,6.55099702771811));
#185285=CARTESIAN_POINT('Ctrl Pts',(19.3514689484114,21.2359584701578,6.55064059397496));
#185286=CARTESIAN_POINT('Ctrl Pts',(19.3395091927779,21.2395684829232,6.54989376929634));
#185287=CARTESIAN_POINT('Ctrl Pts',(19.333261525781,21.2414228856798,6.54950323201497));
#185288=CARTESIAN_POINT('Ctrl Pts',(19.3184058901224,21.2457577263047,6.54857361618221));
#185289=CARTESIAN_POINT('Ctrl Pts',(19.3097905953382,21.2482124178963,6.54803370463748));
#185290=CARTESIAN_POINT('Ctrl Pts',(19.2808434871231,21.2562618124179,6.54621681249706));
#185291=CARTESIAN_POINT('Ctrl Pts',(19.2604442186606,21.2616072551544,6.54493178864399));
#185292=CARTESIAN_POINT('Ctrl Pts',(19.1497962395621,21.2888417250806,6.53793449411119));
#185293=CARTESIAN_POINT('Ctrl Pts',(19.0582726050505,21.3050764277848,6.53204281257723));
#185294=CARTESIAN_POINT('Ctrl Pts',(18.8139508063882,21.3320123496317,6.51608926787609));
#185295=CARTESIAN_POINT('Ctrl Pts',(18.6605552268599,21.3322467211271,6.50581704810741));
#185296=CARTESIAN_POINT('Ctrl Pts',(18.5039746660936,21.3154709224792,6.49562541670175));
#185297=CARTESIAN_POINT('Ctrl Pts',(18.499472319018,21.3149739269096,6.4953326543284));
#185298=CARTESIAN_POINT('Ctrl Pts',(18.4885904756535,21.3137373610616,6.49462581937674));
#185299=CARTESIAN_POINT('Ctrl Pts',(18.4822126514723,21.3129832008865,6.49421216893194));
#185300=CARTESIAN_POINT('Ctrl Pts',(18.4308574777154,21.3066735023005,6.49088690304002));
#185301=CARTESIAN_POINT('Ctrl Pts',(18.3860619035265,21.2997035613455,6.48802024245565));
#185302=CARTESIAN_POINT('Ctrl Pts',(18.3340481782807,21.2898904190966,6.48475743232259));
#185303=CARTESIAN_POINT('Ctrl Pts',(18.3265826491635,21.2884402375357,6.48429072076943));
#185304=CARTESIAN_POINT('Ctrl Pts',(18.3146117237332,21.2860478685214,6.48354510019041));
#185305=CARTESIAN_POINT('Ctrl Pts',(18.3101013822464,21.2851311785215,6.48326479697567));
#185306=CARTESIAN_POINT('Ctrl Pts',(18.3020856641791,21.283474810614,6.48276780705407));
#185307=CARTESIAN_POINT('Ctrl Pts',(18.2985791368152,21.2827409362016,6.48255079324164));
#185308=CARTESIAN_POINT('Ctrl Pts',(18.2911140330452,21.281158788451,6.48208964836945));
#185309=CARTESIAN_POINT('Ctrl Pts',(18.2871560316332,21.2803080625399,6.48184565953584));
#185310=CARTESIAN_POINT('Ctrl Pts',(18.2763982219499,21.2779634928785,6.48118382920562));
#185311=CARTESIAN_POINT('Ctrl Pts',(18.269603233573,21.2764474368937,6.48076724122038));
#185312=CARTESIAN_POINT('Ctrl Pts',(18.234820074199,21.2685065026646,6.47864159410593));
#185313=CARTESIAN_POINT('Ctrl Pts',(18.2069557717729,21.2615458230706,6.47696150413894));
#185314=CARTESIAN_POINT('Ctrl Pts',(18.1252214153121,21.2393517498978,6.47207754846553));
#185315=CARTESIAN_POINT('Ctrl Pts',(18.0718017058866,21.2225457941321,6.46894254634176));
#185316=CARTESIAN_POINT('Ctrl Pts',(17.8360824269301,21.1379776622748,6.45511667775489));
#185317=CARTESIAN_POINT('Ctrl Pts',(17.6629847613231,21.0474170405242,6.44488900683143));
#185318=CARTESIAN_POINT('Ctrl Pts',(17.471835043354,20.9110752380083,6.43145748909968));
#185319=CARTESIAN_POINT('Ctrl Pts',(17.4396724908183,20.886718406742,6.4291186621684));
#185320=CARTESIAN_POINT('Ctrl Pts',(17.3989225789456,20.8539849986759,6.42604110602431));
#185321=CARTESIAN_POINT('Ctrl Pts',(17.3896819009965,20.8464327457826,6.42533534593917));
#185322=CARTESIAN_POINT('Ctrl Pts',(17.37501017457,20.8342334198388,6.42420186880182));
#185323=CARTESIAN_POINT('Ctrl Pts',(17.3695378641247,20.829636203334,6.42377618270377));
#185324=CARTESIAN_POINT('Ctrl Pts',(17.3593292881262,20.8209715553607,6.42297652386949));
#185325=CARTESIAN_POINT('Ctrl Pts',(17.3545875207941,20.8169107030192,6.42260282429352));
#185326=CARTESIAN_POINT('Ctrl Pts',(17.3439205614068,20.8076934116243,6.42175698184209));
#185327=CARTESIAN_POINT('Ctrl Pts',(17.338005989974,20.802524871845,6.4212843391931));
#185328=CARTESIAN_POINT('Ctrl Pts',(17.3206339557985,20.7871727073747,6.4198852180242));
#185329=CARTESIAN_POINT('Ctrl Pts',(17.3092583675527,20.7768975827782,6.41895491115518));
#185330=CARTESIAN_POINT('Ctrl Pts',(17.2835628868592,20.7531760639361,6.4168205525066));
#185331=CARTESIAN_POINT('Ctrl Pts',(17.2693167107258,20.7396522341121,6.4156132496631));
#185332=CARTESIAN_POINT('Ctrl Pts',(17.2233142577662,20.6947488369198,6.41163455384641));
#185333=CARTESIAN_POINT('Ctrl Pts',(17.1923637336177,20.6625643951854,6.40882909873871));
#185334=CARTESIAN_POINT('Ctrl Pts',(17.1124879833172,20.5740661702069,6.40123614976628));
#185335=CARTESIAN_POINT('Ctrl Pts',(17.0654846546327,20.5161075018084,6.39638472645276));
#185336=CARTESIAN_POINT('Ctrl Pts',(16.9257448224572,20.3238790190281,6.38075997451635));
#185337=CARTESIAN_POINT('Ctrl Pts',(16.8454098971218,20.1813194608543,6.36980564684395));
#185338=CARTESIAN_POINT('Ctrl Pts',(16.7767895748611,20.0179784053648,6.35877883394721));
#185339=CARTESIAN_POINT('Ctrl Pts',(16.771471575353,20.0049578084932,6.35791007378176));
#185340=CARTESIAN_POINT('Ctrl Pts',(16.7642416473625,19.9867394384101,6.35670968001164));
#185341=CARTESIAN_POINT('Ctrl Pts',(16.7622198869111,19.9815860310856,6.35637180607979));
#185342=CARTESIAN_POINT('Ctrl Pts',(16.7590028507478,19.9732903396895,6.35583067912908));
#185343=CARTESIAN_POINT('Ctrl Pts',(16.7577948213683,19.970153076694,6.3556266693372));
#185344=CARTESIAN_POINT('Ctrl Pts',(16.7552832777342,19.963583955137,6.35520083715555));
#185345=CARTESIAN_POINT('Ctrl Pts',(16.7539812120649,19.9601515708852,6.35497910651347));
#185346=CARTESIAN_POINT('Ctrl Pts',(16.7508467966457,19.95182366009,6.35444294816883));
#185347=CARTESIAN_POINT('Ctrl Pts',(16.7490236221209,19.9469246591297,6.35412906756367));
#185348=CARTESIAN_POINT('Ctrl Pts',(16.7466168276675,19.9403834130632,6.35371193039897));
#185349=CARTESIAN_POINT('Ctrl Pts',(16.7460170848424,19.9387471854834,6.35360775105671));
#185350=CARTESIAN_POINT('Ctrl Pts',(16.7454193623257,19.9371102171619,6.35350368608372));
#185351=CARTESIAN_POINT('',(16.6170007251258,19.2092478064746,6.8890562790225));
#185352=CARTESIAN_POINT('Ctrl Pts',(16.6170007251258,19.2092478064745,6.8890562790225));
#185353=CARTESIAN_POINT('Ctrl Pts',(16.6170993834536,19.0900488678703,6.88186870628082));
#185354=CARTESIAN_POINT('Ctrl Pts',(16.6272689227094,18.9712546433195,6.87468113353914));
#185355=CARTESIAN_POINT('Ctrl Pts',(16.6472858251195,18.8541905938,6.86749356079746));
#185356=CARTESIAN_POINT('Ctrl Pts',(16.6595066892529,18.7827198030267,6.86310535186656));
#185357=CARTESIAN_POINT('Ctrl Pts',(16.6754275106646,18.7117380828086,6.85871714293566));
#185358=CARTESIAN_POINT('Ctrl Pts',(16.6949957094315,18.6416578330712,6.85432893400476));
#185359=CARTESIAN_POINT('Ctrl Pts',(16.7145348657469,18.571681594044,6.84994723790349));
#185360=CARTESIAN_POINT('Ctrl Pts',(16.7377105245955,18.5026046302857,6.84556554180222));
#185361=CARTESIAN_POINT('Ctrl Pts',(16.7644188550043,18.4348304867638,6.84118384570095));
#185362=CARTESIAN_POINT('Ctrl Pts',(16.7910958009993,18.3671359832542,6.83680729844131));
#185363=CARTESIAN_POINT('Ctrl Pts',(16.8212969962485,18.3007417053631,6.83243075118166));
#185364=CARTESIAN_POINT('Ctrl Pts',(16.8548689277715,18.2360356860965,6.82805420392202));
#185365=CARTESIAN_POINT('Ctrl Pts',(16.8884195684635,18.171370702447,6.82368043220504));
#185366=CARTESIAN_POINT('Ctrl Pts',(16.9253364824029,18.1083922801994,6.81930666048807));
#185367=CARTESIAN_POINT('Ctrl Pts',(16.9654187837194,18.0474668112084,6.81493288877109));
#185368=CARTESIAN_POINT('Ctrl Pts',(17.005488887857,17.9865598820423,6.81056044800753));
#185369=CARTESIAN_POINT('Ctrl Pts',(17.048722202085,17.9277050686151,6.80618800724398));
#185370=CARTESIAN_POINT('Ctrl Pts',(17.0948736736056,17.87124110896,6.80181556648042));
#185371=CARTESIAN_POINT('Ctrl Pts',(17.1410263252243,17.8147757055153,6.79744301391308));
#185372=CARTESIAN_POINT('Ctrl Pts',(17.1900969754574,17.7607016494436,6.79307046134574));
#185373=CARTESIAN_POINT('Ctrl Pts',(17.24180038849,17.7093244959681,6.7886979087784));
#185374=CARTESIAN_POINT('Ctrl Pts',(17.2935574612749,17.6578940213448,6.78432081821107));
#185375=CARTESIAN_POINT('Ctrl Pts',(17.3479524093388,17.6091663783432,6.77994372764374));
#185376=CARTESIAN_POINT('Ctrl Pts',(17.4046638348792,17.5634095290085,6.77556663707641));
#185377=CARTESIAN_POINT('Ctrl Pts',(17.4614062326339,17.5176276901602,6.77118715601746));
#185378=CARTESIAN_POINT('Ctrl Pts',(17.5204672358497,17.4748201585677,6.76680767495852));
#185379=CARTESIAN_POINT('Ctrl Pts',(17.5814953303095,17.435212291308,6.76242819389957));
#185380=CARTESIAN_POINT('Ctrl Pts',(17.6426315966571,17.3955342193695,6.75804095023985));
#185381=CARTESIAN_POINT('Ctrl Pts',(17.7057414989266,17.3590673788383,6.75365370658012));
#185382=CARTESIAN_POINT('Ctrl Pts',(17.7704482580139,17.3259915012087,6.7492664629204));
#185383=CARTESIAN_POINT('Ctrl Pts',(17.8144426190643,17.3035030916047,6.7462835599856));
#185384=CARTESIAN_POINT('Ctrl Pts',(17.8591746727796,17.2825812380498,6.74330065705081));
#185385=CARTESIAN_POINT('Ctrl Pts',(17.9045214391032,17.2632694444527,6.74031775411601));
#185386=CARTESIAN_POINT('Ctrl Pts',(17.971231985614,17.2348594737004,6.73592954518512));
#185387=CARTESIAN_POINT('Ctrl Pts',(18.0395340178844,17.2098253061038,6.73154133625423));
#185388=CARTESIAN_POINT('Ctrl Pts',(18.1090523123257,17.1883459545264,6.72715312732333));
#185389=CARTESIAN_POINT('Ctrl Pts',(18.1784674300917,17.1668984818681,6.72277143122207));
#185390=CARTESIAN_POINT('Ctrl Pts',(18.2490947695194,17.1489954929982,6.7183897351208));
#185391=CARTESIAN_POINT('Ctrl Pts',(18.3205388114172,17.1347681137369,6.71400803901954));
#185392=CARTESIAN_POINT('Ctrl Pts',(18.39189890088,17.1205574527785,6.7096314917599));
#185393=CARTESIAN_POINT('Ctrl Pts',(18.4640733156415,17.1100139151849,6.70525494450027));
#185394=CARTESIAN_POINT('Ctrl Pts',(18.5366526876863,17.1032184557401,6.70087839724063));
#185395=CARTESIAN_POINT('Ctrl Pts',(18.6091860309483,17.096427305877,6.69650462552366));
#185396=CARTESIAN_POINT('Ctrl Pts',(18.6821233428378,17.0933795627893,6.69213085380669));
#185397=CARTESIAN_POINT('Ctrl Pts',(18.7550478100762,17.0941046342129,6.68775708208972));
#185398=CARTESIAN_POINT('Ctrl Pts',(18.8279500861543,17.0948294849947,6.68338464132617));
#185399=CARTESIAN_POINT('Ctrl Pts',(18.9008390432773,17.0993248662018,6.67901220056263));
#185400=CARTESIAN_POINT('Ctrl Pts',(18.973297213934,17.1075680796842,6.67463975979908));
#185401=CARTESIAN_POINT('Ctrl Pts',(19.0457572373541,17.1158115039465,6.67026720723174));
#185402=CARTESIAN_POINT('Ctrl Pts',(19.1177859733783,17.1278028942377,6.66589465466439));
#185403=CARTESIAN_POINT('Ctrl Pts',(19.1889721056822,17.1434678036241,6.66152210209705));
#185404=CARTESIAN_POINT('Ctrl Pts',(19.2602321176392,17.1591489706443,6.65714501152973));
#185405=CARTESIAN_POINT('Ctrl Pts',(19.330647307792,17.1785111648148,6.6527679209624));
#185406=CARTESIAN_POINT('Ctrl Pts',(19.3998183959317,17.2014291842189,6.64839083039508));
#185407=CARTESIAN_POINT('Ctrl Pts',(19.4690272609699,17.2243597200041,6.64401134933614));
#185408=CARTESIAN_POINT('Ctrl Pts',(19.5369902214606,17.2508497721601,6.6396318682772));
#185409=CARTESIAN_POINT('Ctrl Pts',(19.6033275197868,17.2807257543703,6.63525238721827));
#185410=CARTESIAN_POINT('Ctrl Pts',(19.6697824005289,17.3106546915584,6.63086514355855));
#185411=CARTESIAN_POINT('Ctrl Pts',(19.7346054355376,17.3439813228772,6.62647789989883));
#185412=CARTESIAN_POINT('Ctrl Pts',(19.7974415556861,17.3804861219756,6.62209065623912));
#185413=CARTESIAN_POINT('Ctrl Pts',(19.8401640625133,17.4053058677686,6.61910775330427));
#185414=CARTESIAN_POINT('Ctrl Pts',(19.8819686426642,17.4315938434276,6.61612485036943));
#185415=CARTESIAN_POINT('Ctrl Pts',(19.922752149464,17.4592701900279,6.61314194743459));
#185416=CARTESIAN_POINT('Ctrl Pts',(19.982749592452,17.4999854241401,6.60875373850369));
#185417=CARTESIAN_POINT('Ctrl Pts',(20.0407699602753,17.5438661041391,6.60436552957279));
#185418=CARTESIAN_POINT('Ctrl Pts',(20.0964596300332,17.590693622635,6.5999773206419));
#185419=CARTESIAN_POINT('Ctrl Pts',(20.1520666470877,17.6374516413292,6.59559562454063));
#185420=CARTESIAN_POINT('Ctrl Pts',(20.2053494667967,17.6871475084509,6.59121392843937));
#185421=CARTESIAN_POINT('Ctrl Pts',(20.2559837460597,17.7395196308717,6.5868322323381));
#185422=CARTESIAN_POINT('Ctrl Pts',(20.306558526015,17.7918302118807,6.58245568507846));
#185423=CARTESIAN_POINT('Ctrl Pts',(20.3544906143945,17.8468104559209,6.57807913781883));
#185424=CARTESIAN_POINT('Ctrl Pts',(20.3994903578941,17.9041599685647,6.57370259055919));
#185425=CARTESIAN_POINT('Ctrl Pts',(20.4444615632103,17.961473110981,6.56932881884221));
#185426=CARTESIAN_POINT('Ctrl Pts',(20.4865038163914,18.0211521621719,6.56495504712524));
#185427=CARTESIAN_POINT('Ctrl Pts',(20.5253667770635,18.0828625659818,6.56058127540827));
#185428=CARTESIAN_POINT('Ctrl Pts',(20.5642179116062,18.1445541911086,6.55620883464472));
#185429=CARTESIAN_POINT('Ctrl Pts',(20.5998914174628,18.2082755337073,6.55183639388117));
#185430=CARTESIAN_POINT('Ctrl Pts',(20.6321804129395,18.2736632835887,6.54746395311761));
#185431=CARTESIAN_POINT('Ctrl Pts',(20.6644702340494,18.339052705442,6.54309140055027));
#185432=CARTESIAN_POINT('Ctrl Pts',(20.69337516117,18.4061081857736,6.53871884798293));
#185433=CARTESIAN_POINT('Ctrl Pts',(20.7187351546659,18.4744435759338,6.53434629541559));
#185434=CARTESIAN_POINT('Ctrl Pts',(20.7441214677198,18.5428498871395,6.52996920484826));
#185435=CARTESIAN_POINT('Ctrl Pts',(20.765955333456,18.6125383070841,6.52559211428094));
#185436=CARTESIAN_POINT('Ctrl Pts',(20.7841259040689,18.6831053348765,6.52121502371361));
#185437=CARTESIAN_POINT('Ctrl Pts',(20.8023063983048,18.7537109019418,6.51683554265467));
#185438=CARTESIAN_POINT('Ctrl Pts',(20.8168195180773,18.8251955591513,6.51245606159573));
#185439=CARTESIAN_POINT('Ctrl Pts',(20.8276056664128,18.8971460314662,6.50807658053679));
#185440=CARTESIAN_POINT('Ctrl Pts',(20.8384109331237,18.9692240355102,6.50368933687707));
#185441=CARTESIAN_POINT('Ctrl Pts',(20.8454759896224,19.0417690229281,6.49930209321735));
#185442=CARTESIAN_POINT('Ctrl Pts',(20.8487932306455,19.1143636113251,6.49491484955763));
#185443=CARTESIAN_POINT('Ctrl Pts',(20.8510486348926,19.1637209362373,6.4919319466228));
#185444=CARTESIAN_POINT('Ctrl Pts',(20.8515726338748,19.213101155059,6.48894904368798));
#185445=CARTESIAN_POINT('Ctrl Pts',(20.8503765449711,19.2623743116388,6.48596614075315));
#185446=CARTESIAN_POINT('Ctrl Pts',(20.8486169543561,19.33486105039,6.48157793182225));
#185447=CARTESIAN_POINT('Ctrl Pts',(20.8431255714045,19.4073987776277,6.47718972289135));
#185448=CARTESIAN_POINT('Ctrl Pts',(20.8338948009668,19.4795718244205,6.47280151396045));
#185449=CARTESIAN_POINT('Ctrl Pts',(20.8246777305229,19.5516377544454,6.46841981785919));
#185450=CARTESIAN_POINT('Ctrl Pts',(20.8117323505349,19.623339603948,6.46403812175792));
#185451=CARTESIAN_POINT('Ctrl Pts',(20.7951030586571,19.6942630563103,6.45965642565665));
#185452=CARTESIAN_POINT('Ctrl Pts',(20.7784933075206,19.7651031679718,6.45527987839701));
#185453=CARTESIAN_POINT('Ctrl Pts',(20.7582083534309,19.8351662321977,6.45090333113737));
#185454=CARTESIAN_POINT('Ctrl Pts',(20.7343439967233,19.9040460985916,6.44652678387773));
#185455=CARTESIAN_POINT('Ctrl Pts',(20.7104947744439,19.9728822823753,6.44215301216075));
#185456=CARTESIAN_POINT('Ctrl Pts',(20.6830708110594,20.0405363024768,6.43777924044378));
#185457=CARTESIAN_POINT('Ctrl Pts',(20.6522179108558,20.1066165733571,6.4334054687268));
#185458=CARTESIAN_POINT('Ctrl Pts',(20.6213743992934,20.172676735789,6.42903302796325));
#185459=CARTESIAN_POINT('Ctrl Pts',(20.5871042264077,20.2371636629376,6.4246605871997));
#185460=CARTESIAN_POINT('Ctrl Pts',(20.5496008974355,20.2997067471232,6.42028814643614));
#185461=CARTESIAN_POINT('Ctrl Pts',(20.512096609499,20.3622514305424,6.4159155938688));
#185462=CARTESIAN_POINT('Ctrl Pts',(20.471359251125,20.4228517596427,6.41154304130145));
#185463=CARTESIAN_POINT('Ctrl Pts',(20.4276268857992,20.4811641514774,6.40717048873411));
#185464=CARTESIAN_POINT('Ctrl Pts',(20.3838491333751,20.5395370621118,6.40279339816678));
#185465=CARTESIAN_POINT('Ctrl Pts',(20.3370704580442,20.5956169078824,6.39841630759945));
#185466=CARTESIAN_POINT('Ctrl Pts',(20.2875701403857,20.6490920759472,6.39403921703212));
#185467=CARTESIAN_POINT('Ctrl Pts',(20.2380427887665,20.7025964487859,6.38965973597318));
#185468=CARTESIAN_POINT('Ctrl Pts',(20.1857911812153,20.7534929748974,6.38528025491424));
#185469=CARTESIAN_POINT('Ctrl Pts',(20.1311305579261,20.8015078447179,6.38090077385529));
#185470=CARTESIAN_POINT('Ctrl Pts',(20.076373049049,20.8496078205729,6.37651353019557));
#185471=CARTESIAN_POINT('Ctrl Pts',(20.0191983762069,20.8948156407836,6.37212628653585));
#185472=CARTESIAN_POINT('Ctrl Pts',(19.9599533753571,20.9368989893533,6.36773904287613));
#185473=CARTESIAN_POINT('Ctrl Pts',(19.919672483614,20.9655116112387,6.36475613994132));
#185474=CARTESIAN_POINT('Ctrl Pts',(19.878435164885,20.9926807873361,6.36177323700652));
#185475=CARTESIAN_POINT('Ctrl Pts',(19.8363568176098,21.0183456909704,6.35879033407171));
#185476=CARTESIAN_POINT('Ctrl Pts',(19.7744545085685,21.0561018505907,6.35440212514082));
#185477=CARTESIAN_POINT('Ctrl Pts',(19.7104893778665,21.0907477625256,6.35001391620992));
#185478=CARTESIAN_POINT('Ctrl Pts',(19.6448068261836,21.1220520467474,6.34562570727902));
#185479=CARTESIAN_POINT('Ctrl Pts',(19.5792217582976,21.1533098702211,6.34124401117775));
#185480=CARTESIAN_POINT('Ctrl Pts',(19.5119247612707,21.1812357055046,6.33686231507649));
#185481=CARTESIAN_POINT('Ctrl Pts',(19.4432882414197,21.2056426222719,6.33248061897522));
#185482=CARTESIAN_POINT('Ctrl Pts',(19.3747323749418,21.2300208589696,6.32810407171558));
#185483=CARTESIAN_POINT('Ctrl Pts',(19.3048405647339,21.2508882305582,6.32372752445594));
#185484=CARTESIAN_POINT('Ctrl Pts',(19.2340061739094,21.2681054484524,6.3193509771963));
#185485=CARTESIAN_POINT('Ctrl Pts',(19.163216705226,21.2853117474372,6.31497720547933));
#185486=CARTESIAN_POINT('Ctrl Pts',(19.0914863095581,21.2988723720882,6.31060343376236));
#185487=CARTESIAN_POINT('Ctrl Pts',(19.0192231694687,21.3086979629104,6.30622966204538));
#185488=CARTESIAN_POINT('Ctrl Pts',(18.9469820192955,21.3185205637722,6.30185722128183));
#185489=CARTESIAN_POINT('Ctrl Pts',(18.8742089242432,21.324610322322,6.29748478051827));
#185490=CARTESIAN_POINT('Ctrl Pts',(18.801320247435,21.3269293429331,6.29311233975472));
#185491=CARTESIAN_POINT('Ctrl Pts',(18.7284297068553,21.3292484228418,6.28873978718738));
#185492=CARTESIAN_POINT('Ctrl Pts',(18.6554240608492,21.3277965600419,6.28436723462003));
#185493=CARTESIAN_POINT('Ctrl Pts',(18.5827210675513,21.3225879533179,6.27999468205269));
#185494=CARTESIAN_POINT('Ctrl Pts',(18.5099426203447,21.3173739409054,6.27561759148536));
#185495=CARTESIAN_POINT('Ctrl Pts',(18.4374679351509,21.3083954347152,6.27124050091803));
#185496=CARTESIAN_POINT('Ctrl Pts',(18.3657101983365,21.2957185953962,6.26686341035071));
#185497=CARTESIAN_POINT('Ctrl Pts',(18.2939132719587,21.2830348327847,6.26248392929177));
#185498=CARTESIAN_POINT('Ctrl Pts',(18.2228345439115,21.2666488240855,6.25810444823283));
#185499=CARTESIAN_POINT('Ctrl Pts',(18.1528748782446,21.2466774284903,6.25372496717389));
#185500=CARTESIAN_POINT('Ctrl Pts',(18.0827912095399,21.2266706337304,6.24933772351416));
#185501=CARTESIAN_POINT('Ctrl Pts',(18.0138310210294,21.2030659176044,6.24495047985444));
#185502=CARTESIAN_POINT('Ctrl Pts',(17.9463773894269,21.1760291660212,6.24056323619472));
#185503=CARTESIAN_POINT('Ctrl Pts',(17.9005154197537,21.1576467801999,6.23758033325991));
#185504=CARTESIAN_POINT('Ctrl Pts',(17.8553494637706,21.1376788808132,6.23459743032509));
#185505=CARTESIAN_POINT('Ctrl Pts',(17.810993130072,21.1161895753614,6.23161452739028));
#185506=CARTESIAN_POINT('Ctrl Pts',(17.7457580547162,21.0845851494857,6.22722755755968));
#185507=CARTESIAN_POINT('Ctrl Pts',(17.6820207921133,21.0495646312793,6.22284058772908));
#185508=CARTESIAN_POINT('Ctrl Pts',(17.6201625345974,21.0112930596615,6.21845361789848));
#185509=CARTESIAN_POINT('Ctrl Pts',(17.5583882674481,20.973073452704,6.21407260464052));
#185510=CARTESIAN_POINT('Ctrl Pts',(17.4984883504397,20.9316118007434,6.20969159138257));
#185511=CARTESIAN_POINT('Ctrl Pts',(17.4408213800117,20.8871199410559,6.20531057812461));
#185512=CARTESIAN_POINT('Ctrl Pts',(17.3832136794392,20.8426738099037,6.20093406765258));
#185513=CARTESIAN_POINT('Ctrl Pts',(17.3278347507055,20.7952039448586,6.19655755718055));
#185514=CARTESIAN_POINT('Ctrl Pts',(17.2750146386712,20.744965682611,6.19218104670852));
#185515=CARTESIAN_POINT('Ctrl Pts',(17.2222313878241,20.694762479774,6.18780759044001));
#185516=CARTESIAN_POINT('Ctrl Pts',(17.1720037564642,20.641795047518,6.18343413417149));
#185517=CARTESIAN_POINT('Ctrl Pts',(17.1246277766866,20.5863581522015,6.17906067790298));
#185518=CARTESIAN_POINT('Ctrl Pts',(17.0772569743077,20.5309273152064,6.17468769957978));
#185519=CARTESIAN_POINT('Ctrl Pts',(17.032737527321,20.4730279095102,6.17031472125657));
#185520=CARTESIAN_POINT('Ctrl Pts',(16.9913267830634,20.4129896251515,6.16594174293336));
#185521=CARTESIAN_POINT('Ctrl Pts',(16.9499189762244,20.3529555995323,6.16156907480182));
#185522=CARTESIAN_POINT('Ctrl Pts',(16.9116197015745,20.290783398272,6.15719640667029));
#185523=CARTESIAN_POINT('Ctrl Pts',(16.8766431790035,20.2268319937361,6.15282373853875));
#185524=CARTESIAN_POINT('Ctrl Pts',(16.8416426205659,20.1628366417943,6.14844806550962));
#185525=CARTESIAN_POINT('Ctrl Pts',(16.8099695961625,20.0970600736454,6.14407239248049));
#185526=CARTESIAN_POINT('Ctrl Pts',(16.7817919876605,20.0298851424696,6.13969671945136));
#185527=CARTESIAN_POINT('Ctrl Pts',(16.7689367260135,19.9992384211085,6.13770043855097));
#185528=CARTESIAN_POINT('Ctrl Pts',(16.7568083349981,19.9683009234817,6.13570415765058));
#185529=CARTESIAN_POINT('Ctrl Pts',(16.7454193623258,19.9371102171621,6.13370787675019));
#185530=CARTESIAN_POINT('Ctrl Pts',(16.7486737101886,19.9359290495398,6.93361858560548));
#185531=CARTESIAN_POINT('Ctrl Pts',(16.6638908325239,19.7029525058723,6.91876473928283));
#185532=CARTESIAN_POINT('Ctrl Pts',(16.617844370368,19.4557557402532,6.90391089296018));
#185533=CARTESIAN_POINT('Ctrl Pts',(16.6156461087368,19.2092594235966,6.88905704663753));
#185534=CARTESIAN_POINT('Origin',(18.734,19.211,0.));
#185535=CARTESIAN_POINT('',(16.7454193311435,19.9371101317641,7.95734462820299));
#185536=CARTESIAN_POINT('',(16.7454193726884,19.9371102455419,7.73405220823975));
#185537=CARTESIAN_POINT('',(16.7454193623258,19.9371102171621,0.));
#185538=CARTESIAN_POINT('',(16.617000799818,19.2090893184087,7.91072951538306));
#185539=CARTESIAN_POINT('Ctrl Pts',(16.7454193311435,19.9371101317641,7.95734462820299));
#185540=CARTESIAN_POINT('Ctrl Pts',(16.7388878108518,19.9192224114001,7.95624410831949));
#185541=CARTESIAN_POINT('Ctrl Pts',(16.732595939587,19.9012418899709,7.95513586263103));
#185542=CARTESIAN_POINT('Ctrl Pts',(16.7220479121879,19.8697400685245,7.95318935666933));
#185543=CARTESIAN_POINT('Ctrl Pts',(16.7176850003347,19.8562623413191,7.95235503299141));
#185544=CARTESIAN_POINT('Ctrl Pts',(16.7109454732511,19.8347068686673,7.95101780437524));
#185545=CARTESIAN_POINT('Ctrl Pts',(16.7084811681145,19.8266568319897,7.95051777631579));
#185546=CARTESIAN_POINT('Ctrl Pts',(16.7042134956983,19.8124128052234,7.94963180975945));
#185547=CARTESIAN_POINT('Ctrl Pts',(16.7023902911245,19.8062248354304,7.94924652551381));
#185548=CARTESIAN_POINT('Ctrl Pts',(16.698671963352,19.7933886782359,7.94844643859772));
#185549=CARTESIAN_POINT('Ctrl Pts',(16.6967810667854,19.7867393556909,7.94803150335748));
#185550=CARTESIAN_POINT('Ctrl Pts',(16.6919990780092,19.7696049843739,7.94696098844802));
#185551=CARTESIAN_POINT('Ctrl Pts',(16.6891561857431,19.7591067983157,7.94630385146098));
#185552=CARTESIAN_POINT('Ctrl Pts',(16.6831808743635,19.7363475538504,7.94487640696553));
#185553=CARTESIAN_POINT('Ctrl Pts',(16.6800772595627,19.724079432261,7.94410519509892));
#185554=CARTESIAN_POINT('Ctrl Pts',(16.6713661718758,19.688299612147,7.94185059233987));
#185555=CARTESIAN_POINT('Ctrl Pts',(16.6660512902545,19.6647193927235,7.94035798085899));
#185556=CARTESIAN_POINT('Ctrl Pts',(16.631655769437,19.4989331522908,7.92981457930352));
#185557=CARTESIAN_POINT('Ctrl Pts',(16.6168699507311,19.3541831232757,7.92031685552876));
#185558=CARTESIAN_POINT('Ctrl Pts',(16.6170008616849,19.2090899284988,7.91072944747406));
#185559=CARTESIAN_POINT('Ctrl Pts',(16.617000862229,19.2090893255851,7.91072940763498));
#185560=CARTESIAN_POINT('Ctrl Pts',(16.6171115217323,19.0864802242008,7.90262769413136));
#185561=CARTESIAN_POINT('Ctrl Pts',(16.6278735760837,18.9640980518275,7.8945060011454));
#185562=CARTESIAN_POINT('Ctrl Pts',(16.6513555110906,18.8309489058585,7.88604138153807));
#185563=CARTESIAN_POINT('Ctrl Pts',(16.6536481219582,18.8185933470417,7.88525964032872));
#185564=CARTESIAN_POINT('Ctrl Pts',(16.6573287545432,18.7996969149763,7.88407053382136));
#185565=CARTESIAN_POINT('Ctrl Pts',(16.6586379308329,18.793141203293,7.88365919776567));
#185566=CARTESIAN_POINT('Ctrl Pts',(16.6608486749733,18.782337616983,7.88298343355589));
#185567=CARTESIAN_POINT('Ctrl Pts',(16.6617322869808,18.7780861732261,7.88271804429092));
#185568=CARTESIAN_POINT('Ctrl Pts',(16.6634789751564,18.7698099859251,7.88220250717016));
#185569=CARTESIAN_POINT('Ctrl Pts',(16.66434072053,18.7657849840704,7.88195228641702));
#185570=CARTESIAN_POINT('Ctrl Pts',(16.6659719859702,18.7582728359787,7.88148625496955));
#185571=CARTESIAN_POINT('Ctrl Pts',(16.6667385813809,18.7547851611577,7.88127028640043));
#185572=CARTESIAN_POINT('Ctrl Pts',(16.6685067296264,18.7468368285494,7.88077898700932));
#185573=CARTESIAN_POINT('Ctrl Pts',(16.669513906878,18.7423774739779,7.88050398209707));
#185574=CARTESIAN_POINT('Ctrl Pts',(16.672647297999,18.7287103141891,7.8796629908247));
#185575=CARTESIAN_POINT('Ctrl Pts',(16.6748207597799,18.719513309208,7.87909964645304));
#185576=CARTESIAN_POINT('Ctrl Pts',(16.7060513545,18.591205808496,7.87127263433017));
#185577=CARTESIAN_POINT('Ctrl Pts',(16.7453452243574,18.4748060097416,7.86455349602807));
#185578=CARTESIAN_POINT('Ctrl Pts',(16.8230773833356,18.2971367491519,7.85400318070861));
#185579=CARTESIAN_POINT('Ctrl Pts',(16.854933174031,18.2333093464563,7.85014914108799));
#185580=CARTESIAN_POINT('Ctrl Pts',(16.9337303111766,18.0935635691121,7.84135922203372));
#185581=CARTESIAN_POINT('Ctrl Pts',(16.9823694337745,18.0187654453276,7.83640085431816));
#185582=CARTESIAN_POINT('Ctrl Pts',(17.0559433438922,17.9198845367816,7.82930991886426));
#185583=CARTESIAN_POINT('Ctrl Pts',(17.0769701061936,17.8930072010336,7.82732372237705));
#185584=CARTESIAN_POINT('Ctrl Pts',(17.1055478167489,17.8582432064424,7.8246699426616));
#185585=CARTESIAN_POINT('Ctrl Pts',(17.1125238996734,17.8498891650469,7.82402556213667));
#185586=CARTESIAN_POINT('Ctrl Pts',(17.1240368074629,17.8363162798019,7.82296749191349));
#185587=CARTESIAN_POINT('Ctrl Pts',(17.1285353880166,17.8310651501514,7.82255537444089));
#185588=CARTESIAN_POINT('Ctrl Pts',(17.1372800805119,17.8209582359015,7.82175674696685));
#185589=CARTESIAN_POINT('Ctrl Pts',(17.1415228233908,17.8160996280098,7.82137037924043));
#185590=CARTESIAN_POINT('Ctrl Pts',(17.1513515164192,17.8049475159386,7.82047782489024));
#185591=CARTESIAN_POINT('Ctrl Pts',(17.1569528912002,17.7986678068003,7.81997099516518));
#185592=CARTESIAN_POINT('Ctrl Pts',(17.1720751254772,17.7819163817515,7.81860748511263));
#185593=CARTESIAN_POINT('Ctrl Pts',(17.1816636786611,17.7715066058566,7.81774794787695));
#185594=CARTESIAN_POINT('Ctrl Pts',(17.2658241721346,17.6819569003964,7.81024558095259));
#185595=CARTESIAN_POINT('Ctrl Pts',(17.3462751126359,17.6085873372018,7.80334315202871));
#185596=CARTESIAN_POINT('Ctrl Pts',(17.5090293811134,17.4816414482223,7.78990320663323));
#185597=CARTESIAN_POINT('Ctrl Pts',(17.5901303824558,17.4269610761572,7.78341790655111));
#185598=CARTESIAN_POINT('Ctrl Pts',(17.73695210681,17.3421093970625,7.77224084308671));
#185599=CARTESIAN_POINT('Ctrl Pts',(17.8009879643803,17.3093305855095,7.7675369343157));
#185600=CARTESIAN_POINT('Ctrl Pts',(17.8972779810167,17.2660788198424,7.76082201600904));
#185601=CARTESIAN_POINT('Ctrl Pts',(17.9283111977942,17.2530194117084,7.7587104101043));
#185602=CARTESIAN_POINT('Ctrl Pts',(17.9664251261026,17.2380400689219,7.75619157376596));
#185603=CARTESIAN_POINT('Ctrl Pts',(17.9732194597741,17.2354102020303,7.75574540180616));
#185604=CARTESIAN_POINT('Ctrl Pts',(17.9839075088589,17.2313365191189,7.75504814815731));
#185605=CARTESIAN_POINT('Ctrl Pts',(17.9877920522528,17.2298690244703,7.75479568550417));
#185606=CARTESIAN_POINT('Ctrl Pts',(17.9950210375755,17.2271623520456,7.75432766455028));
#185607=CARTESIAN_POINT('Ctrl Pts',(17.9983642606297,17.2259202082591,7.75411193498586));
#185608=CARTESIAN_POINT('Ctrl Pts',(18.0059514155221,17.2231230705309,7.75362396853561));
#185609=CARTESIAN_POINT('Ctrl Pts',(18.0101971870373,17.2215732190168,7.75335204009516));
#185610=CARTESIAN_POINT('Ctrl Pts',(18.0228092672688,17.2170150990527,7.75254755588709));
#185611=CARTESIAN_POINT('Ctrl Pts',(18.031189718727,17.2140458797639,7.75201726636002));
#185612=CARTESIAN_POINT('Ctrl Pts',(18.0942308656191,17.1921562230908,7.74805845901932));
#185613=CARTESIAN_POINT('Ctrl Pts',(18.1496329269367,17.1754285487274,7.74474933848112));
#185614=CARTESIAN_POINT('Ctrl Pts',(18.3637038705559,17.1202565307368,7.73236201565668));
#185615=CARTESIAN_POINT('Ctrl Pts',(18.5259378756946,17.0979349238789,7.72375541159319));
#185616=CARTESIAN_POINT('Ctrl Pts',(18.7491666387576,17.0932029041039,7.71138758736893));
#185617=CARTESIAN_POINT('Ctrl Pts',(18.809222593072,17.0944850986797,7.70801388948652));
#185618=CARTESIAN_POINT('Ctrl Pts',(18.8932766284678,17.0998616995016,7.70317726402674));
#185619=CARTESIAN_POINT('Ctrl Pts',(18.9173844496788,17.101819105777,7.70177689500875));
#185620=CARTESIAN_POINT('Ctrl Pts',(18.9594310889119,17.1059593405741,7.69930852682522));
#185621=CARTESIAN_POINT('Ctrl Pts',(18.9773855763199,17.1079596330659,7.69824619818415));
#185622=CARTESIAN_POINT('Ctrl Pts',(19.0037823945268,17.1112430332052,7.69667127659739));
#185623=CARTESIAN_POINT('Ctrl Pts',(19.0122463789486,17.1123478588993,7.69616430280104));
#185624=CARTESIAN_POINT('Ctrl Pts',(19.0270904075126,17.1143768651399,7.6952716034625));
#185625=CARTESIAN_POINT('Ctrl Pts',(19.0334733817576,17.115279062278,7.69488657759882));
#185626=CARTESIAN_POINT('Ctrl Pts',(19.0458714900072,17.1170892618334,7.69413641485472));
#185627=CARTESIAN_POINT('Ctrl Pts',(19.0518870325934,17.1179940661822,7.69377138287367));
#185628=CARTESIAN_POINT('Ctrl Pts',(19.0662773475747,17.1202219985307,7.69289559644162));
#185629=CARTESIAN_POINT('Ctrl Pts',(19.0746481857973,17.1215695279861,7.69238407203286));
#185630=CARTESIAN_POINT('Ctrl Pts',(19.1049399112946,17.1266327310313,7.69052533810902));
#185631=CARTESIAN_POINT('Ctrl Pts',(19.1268094194446,17.1306432924681,7.68916880568582));
#185632=CARTESIAN_POINT('Ctrl Pts',(19.3293663327736,17.1710971629178,7.67646435629404));
#185633=CARTESIAN_POINT('Ctrl Pts',(19.5046006152226,17.230643392469,7.6643295609358));
#185634=CARTESIAN_POINT('Ctrl Pts',(19.7425193903469,17.3479010943798,7.64681543233594));
#185635=CARTESIAN_POINT('Ctrl Pts',(19.813058936558,17.3878482103719,7.6414918430162));
#185636=CARTESIAN_POINT('Ctrl Pts',(19.9116121747825,17.4513883595351,7.63401541462695));
#185637=CARTESIAN_POINT('Ctrl Pts',(19.9415771187918,17.471815873412,7.63173714904231));
#185638=CARTESIAN_POINT('Ctrl Pts',(19.9770746693954,17.4973750946249,7.62904597482545));
#185639=CARTESIAN_POINT('Ctrl Pts',(19.983121743143,17.5017780060331,7.62858780921532));
#185640=CARTESIAN_POINT('Ctrl Pts',(19.9924972828569,17.5086807251005,7.62787806080525));
#185641=CARTESIAN_POINT('Ctrl Pts',(19.9958418576696,17.5111584039757,7.62762498986248));
#185642=CARTESIAN_POINT('Ctrl Pts',(20.0020378979272,17.5157768280971,7.62715641797254));
#185643=CARTESIAN_POINT('Ctrl Pts',(20.004891235833,17.5179148928367,7.62694074215626));
#185644=CARTESIAN_POINT('Ctrl Pts',(20.0113386264253,17.5227715378399,7.62645362944522));
#185645=CARTESIAN_POINT('Ctrl Pts',(20.014929399265,17.5254943838816,7.62618249647196));
#185646=CARTESIAN_POINT('Ctrl Pts',(20.0257620281744,17.5337632652889,7.62536492688483));
#185647=CARTESIAN_POINT('Ctrl Pts',(20.0329768693489,17.5393447420737,7.62482092260802));
#185648=CARTESIAN_POINT('Ctrl Pts',(20.0884419541667,17.5828290430669,7.62064090594019));
#185649=CARTESIAN_POINT('Ctrl Pts',(20.13506466225,17.6227704920059,7.61713931927677));
#185650=CARTESIAN_POINT('Ctrl Pts',(20.2871628311835,17.7649907104421,7.60550236185031));
#185651=CARTESIAN_POINT('Ctrl Pts',(20.3837105533619,17.8761901608859,7.59771483652045));
#185652=CARTESIAN_POINT('Ctrl Pts',(20.5211889403105,18.0724706617717,7.58451615750585));
#185653=CARTESIAN_POINT('Ctrl Pts',(20.5693478086943,18.1518546352064,7.57930758455341));
#185654=CARTESIAN_POINT('Ctrl Pts',(20.621868403324,18.2528319295006,7.57267773426654));
#185655=CARTESIAN_POINT('Ctrl Pts',(20.6313132485968,18.2716728210836,7.5714408340411));
#185656=CARTESIAN_POINT('Ctrl Pts',(20.6443685774546,18.2987165409098,7.56966428107178));
#185657=CARTESIAN_POINT('Ctrl Pts',(20.6482108964007,18.3068065186023,7.56913269454303));
#185658=CARTESIAN_POINT('Ctrl Pts',(20.6547601013541,18.3208246798685,7.56821122626327));
#185659=CARTESIAN_POINT('Ctrl Pts',(20.6574911809295,18.3267414727883,7.56782218713267));
#185660=CARTESIAN_POINT('Ctrl Pts',(20.6626743495707,18.3381082724853,7.56707455997072));
#185661=CARTESIAN_POINT('Ctrl Pts',(20.6651307685882,18.3435562449766,7.56671612569652));
#185662=CARTESIAN_POINT('Ctrl Pts',(20.6714718677267,18.3577802910612,7.56577998228425));
#185663=CARTESIAN_POINT('Ctrl Pts',(20.675319962232,18.3665724368256,7.56520102638198));
#185664=CARTESIAN_POINT('Ctrl Pts',(20.6883056100073,18.3968000533151,7.56320933012567));
#185665=CARTESIAN_POINT('Ctrl Pts',(20.6971487157824,18.4183594622264,7.56178664714834));
#185666=CARTESIAN_POINT('Ctrl Pts',(20.767889126694,18.5992738699959,7.54982639601299));
#185667=CARTESIAN_POINT('Ctrl Pts',(20.8106187325848,18.7654141573428,7.5386255028857));
#185668=CARTESIAN_POINT('Ctrl Pts',(20.8446806213586,19.0242991131105,7.5213705177817));
#185669=CARTESIAN_POINT('Ctrl Pts',(20.850720229395,19.1144216858848,7.51541595429194));
#185670=CARTESIAN_POINT('Ctrl Pts',(20.8511061913673,19.2432841143112,7.50718301448861));
#185671=CARTESIAN_POINT('Ctrl Pts',(20.8501647886522,19.2819077673746,7.50475210883007));
#185672=CARTESIAN_POINT('Ctrl Pts',(20.847772964345,19.3280934375659,7.50190596508729));
#185673=CARTESIAN_POINT('Ctrl Pts',(20.8473379745091,19.335698145387,7.50143930989417));
#185674=CARTESIAN_POINT('Ctrl Pts',(20.8465999622099,19.34748433243,7.50071930156148));
#185675=CARTESIAN_POINT('Ctrl Pts',(20.8463255532801,19.3516674482284,7.50046439151679));
#185676=CARTESIAN_POINT('Ctrl Pts',(20.8457949338566,19.3594043526174,7.49999412722952));
#185677=CARTESIAN_POINT('Ctrl Pts',(20.8455421795424,19.3629582799989,7.49977858728144));
#185678=CARTESIAN_POINT('Ctrl Pts',(20.8449522826184,19.3709669272546,7.49929393457597));
#185679=CARTESIAN_POINT('Ctrl Pts',(20.8446100118803,19.3754212148685,7.49902511257149));
#185680=CARTESIAN_POINT('Ctrl Pts',(20.8435638821703,19.3884936438664,7.4982382441403));
#185681=CARTESIAN_POINT('Ctrl Pts',(20.842821310256,19.3971087149146,7.49772231902875));
#185682=CARTESIAN_POINT('Ctrl Pts',(20.8372749144414,19.4571538914986,7.49414336576038));
#185683=CARTESIAN_POINT('Ctrl Pts',(20.8306425576144,19.508402124951,7.49117532414625));
#185684=CARTESIAN_POINT('Ctrl Pts',(20.818558109384,19.5808386602369,7.48703943721064));
#185685=CARTESIAN_POINT('Ctrl Pts',(20.8146437154506,19.6022606810319,7.48582377884594));
#185686=CARTESIAN_POINT('Ctrl Pts',(20.8014014616075,19.6688989338518,7.48205537020718));
#185687=CARTESIAN_POINT('Ctrl Pts',(20.7909245083259,19.7138737909944,7.47953089308716));
#185688=CARTESIAN_POINT('Ctrl Pts',(20.7507051736267,19.8641062288232,7.47106355087913));
#185689=CARTESIAN_POINT('Ctrl Pts',(20.7142829559303,19.9673901340052,7.46517520783333));
#185690=CARTESIAN_POINT('Ctrl Pts',(20.6477507209412,20.1177993070939,7.45603028383809));
#185691=CARTESIAN_POINT('Ctrl Pts',(20.62349585473,20.1673114422871,7.45292243056156));
#185692=CARTESIAN_POINT('Ctrl Pts',(20.5810528881634,20.2460177949139,7.44777791150813));
#185693=CARTESIAN_POINT('Ctrl Pts',(20.5640366640107,20.2758153920733,7.44578064358734));
#185694=CARTESIAN_POINT('Ctrl Pts',(20.5407177382325,20.3144386498558,7.4431198179861));
#185695=CARTESIAN_POINT('Ctrl Pts',(20.5350602042157,20.3236490793917,7.442479792659));
#185696=CARTESIAN_POINT('Ctrl Pts',(20.5256770236963,20.338665743276,7.44142706254048));
#185697=CARTESIAN_POINT('Ctrl Pts',(20.5219930483793,20.3444978795811,7.44101589916724));
#185698=CARTESIAN_POINT('Ctrl Pts',(20.5148057905447,20.3557538716646,7.44021782827049));
#185699=CARTESIAN_POINT('Ctrl Pts',(20.5113060651358,20.3611799162423,7.43983105615398));
#185700=CARTESIAN_POINT('Ctrl Pts',(20.5031665828489,20.373673678029,7.43893568881556));
#185701=CARTESIAN_POINT('Ctrl Pts',(20.4985092233637,20.38072974523,7.43842643751659));
#185702=CARTESIAN_POINT('Ctrl Pts',(20.4858668726533,20.3996360446069,7.43705217043222));
#185703=CARTESIAN_POINT('Ctrl Pts',(20.4778040668347,20.4114334828779,7.43618422685429));
#185704=CARTESIAN_POINT('Ctrl Pts',(20.4027425062564,20.5189108887095,7.42817964133331));
#185705=CARTESIAN_POINT('Ctrl Pts',(20.3280628889221,20.6089585661001,7.4207414564302));
#185706=CARTESIAN_POINT('Ctrl Pts',(20.1325800255432,20.8085286218215,7.40249413492387));
#185707=CARTESIAN_POINT('Ctrl Pts',(20.0058104253225,20.9111829546335,7.39154528262807));
#185708=CARTESIAN_POINT('Ctrl Pts',(19.840960471985,21.0158254276689,7.37913629671011));
#185709=CARTESIAN_POINT('Ctrl Pts',(19.8129750421383,21.0326941130961,7.37708847206117));
#185710=CARTESIAN_POINT('Ctrl Pts',(19.7783138738562,21.0525075630719,7.37463334315315));
#185711=CARTESIAN_POINT('Ctrl Pts',(19.7720005465251,21.0560735597522,7.37418938613217));
#185712=CARTESIAN_POINT('Ctrl Pts',(19.7620781518832,21.0616110404315,7.37349683595615));
#185713=CARTESIAN_POINT('Ctrl Pts',(19.7584815188524,21.0636045254023,7.37324686678025));
#185714=CARTESIAN_POINT('Ctrl Pts',(19.7517502342958,21.0673098384949,7.37278105434074));
#185715=CARTESIAN_POINT('Ctrl Pts',(19.7486170936688,21.0690241950441,7.37256505471529));
#185716=CARTESIAN_POINT('Ctrl Pts',(19.7414581716295,21.0729178251686,7.37207336199177));
#185717=CARTESIAN_POINT('Ctrl Pts',(19.7374296588107,21.0750919709032,7.37179799684584));
#185718=CARTESIAN_POINT('Ctrl Pts',(19.7250361318013,21.0817288080202,7.37095480790449));
#185719=CARTESIAN_POINT('Ctrl Pts',(19.7166480329933,21.0861484577258,7.37038964621793));
#185720=CARTESIAN_POINT('Ctrl Pts',(19.600814257824,21.146189999056,7.36265694598139));
#185721=CARTESIAN_POINT('Ctrl Pts',(19.4888059933062,21.192565989635,7.35601945123444));
#185722=CARTESIAN_POINT('Ctrl Pts',(19.2028080485743,21.2831834214849,7.33969349807363));
#185723=CARTESIAN_POINT('Ctrl Pts',(19.0260365066536,21.3153841779623,7.3300748064758));
#185724=CARTESIAN_POINT('Ctrl Pts',(18.825876394855,21.3261144537818,7.31840383786235));
#185725=CARTESIAN_POINT('Ctrl Pts',(18.8044107518769,21.326937782776,7.31714348267743));
#185726=CARTESIAN_POINT('Ctrl Pts',(18.7739144161655,21.3276429286495,7.31533909279303));
#185727=CARTESIAN_POINT('Ctrl Pts',(18.7648908388861,21.3277938492569,7.31480347927301));
#185728=CARTESIAN_POINT('Ctrl Pts',(18.7493378589372,21.3279545059123,7.31387724462313));
#185729=CARTESIAN_POINT('Ctrl Pts',(18.7428088206236,21.3279917414165,7.31348748994748));
#185730=CARTESIAN_POINT('Ctrl Pts',(18.7303180282448,21.3280051925998,7.31274003109429));
#185731=CARTESIAN_POINT('Ctrl Pts',(18.72435633362,21.3279864290967,7.31238248810251));
#185732=CARTESIAN_POINT('Ctrl Pts',(18.7088771927129,21.3278723237779,7.31145206210931));
#185733=CARTESIAN_POINT('Ctrl Pts',(18.6993602462742,21.3277379794054,7.31087796217541));
#185734=CARTESIAN_POINT('Ctrl Pts',(18.6670303154439,21.3270635107927,7.30892054943378));
#185735=CARTESIAN_POINT('Ctrl Pts',(18.644225905441,21.3262187282526,7.3075277502134));
#185736=CARTESIAN_POINT('Ctrl Pts',(18.443924244538,21.3155537144721,7.29518344662956));
#185737=CARTESIAN_POINT('Ctrl Pts',(18.2683373114805,21.2837817564082,7.28350739668497));
#185738=CARTESIAN_POINT('Ctrl Pts',(18.0173334272621,21.2048344707143,7.26612445155826));
#185739=CARTESIAN_POINT('Ctrl Pts',(17.9374623963021,21.1742922843585,7.26049814855331));
#185740=CARTESIAN_POINT('Ctrl Pts',(17.8255729331779,21.1235505079833,7.25265695315812));
#185741=CARTESIAN_POINT('Ctrl Pts',(17.7919077536558,21.1071940245427,7.2503038307596));
#185742=CARTESIAN_POINT('Ctrl Pts',(17.7519919185655,21.0864749020348,7.24753652703278));
#185743=CARTESIAN_POINT('Ctrl Pts',(17.7453107277643,21.082961406406,7.24707411322727));
#185744=CARTESIAN_POINT('Ctrl Pts',(17.7349616588027,21.0774481889057,7.24635922919027));
#185745=CARTESIAN_POINT('Ctrl Pts',(17.7312807434323,21.075473261341,7.24610523657316));
#185746=CARTESIAN_POINT('Ctrl Pts',(17.7244699968971,21.0717930771755,7.24563582142066));
#185747=CARTESIAN_POINT('Ctrl Pts',(17.7213386542546,21.0700908268173,7.24542021857355));
#185748=CARTESIAN_POINT('Ctrl Pts',(17.7142752472196,21.0662278990293,7.24493436089347));
#185749=CARTESIAN_POINT('Ctrl Pts',(17.7103457545654,21.0640626312742,7.24466440328963));
#185750=CARTESIAN_POINT('Ctrl Pts',(17.6987856650467,21.0576446844923,7.24387111611506));
#185751=CARTESIAN_POINT('Ctrl Pts',(17.6911743656914,21.0533571891559,7.24334996011801));
#185752=CARTESIAN_POINT('Ctrl Pts',(17.6369037098926,21.0223420881912,7.23964067176655));
#185753=CARTESIAN_POINT('Ctrl Pts',(17.5912469084544,20.9938900257312,7.23655556861603));
#185754=CARTESIAN_POINT('Ctrl Pts',(17.4071719361634,20.869199431522,7.2240564880901));
#185755=CARTESIAN_POINT('Ctrl Pts',(17.2794064816617,20.758340788342,7.21518661704685));
#185756=CARTESIAN_POINT('Ctrl Pts',(17.1115464622912,20.5733265776952,7.20134223797042));
#185757=CARTESIAN_POINT('Ctrl Pts',(17.0604711026317,20.5100720264524,7.19675113267809));
#185758=CARTESIAN_POINT('Ctrl Pts',(17.001725980964,20.4280871239444,7.19086728302855));
#185759=CARTESIAN_POINT('Ctrl Pts',(16.9905151956153,20.4119725404251,7.18971399732614));
#185760=CARTESIAN_POINT('Ctrl Pts',(16.9746597429538,20.3884916612127,7.18803704947961));
#185761=CARTESIAN_POINT('Ctrl Pts',(16.9698336758503,20.3812486614289,7.1875202499984));
#185762=CARTESIAN_POINT('Ctrl Pts',(16.9614964370298,20.3685672856567,7.18661614934196));
#185763=CARTESIAN_POINT('Ctrl Pts',(16.9579652675324,20.3631421479998,7.1862296043861));
#185764=CARTESIAN_POINT('Ctrl Pts',(16.9511894718605,20.3526269340715,7.18548079708145));
#185765=CARTESIAN_POINT('Ctrl Pts',(16.9479416216304,20.3475390022895,7.18511865992843));
#185766=CARTESIAN_POINT('Ctrl Pts',(16.9402801549648,20.3354229593679,7.18425669190227));
#185767=CARTESIAN_POINT('Ctrl Pts',(16.9358860431447,20.3283826869616,7.18375614515876));
#185768=CARTESIAN_POINT('Ctrl Pts',(16.9204543794961,20.3033312277729,7.18197604682077));
#185769=CARTESIAN_POINT('Ctrl Pts',(16.9096454194235,20.2851813358992,7.18068816509537));
#185770=CARTESIAN_POINT('Ctrl Pts',(16.8384380874289,20.1614376846218,7.171916957869));
#185771=CARTESIAN_POINT('Ctrl Pts',(16.7870403045226,20.0510965155842,7.16412180665666));
#185772=CARTESIAN_POINT('Ctrl Pts',(16.7454193167441,19.9371100923285,7.15616136059514));
#185773=CARTESIAN_POINT('',(16.620191220251,19.2105385357295,7.68893962574679));
#185774=CARTESIAN_POINT('Ctrl Pts',(16.6203930058439,19.2105314190313,7.68905589348729));
#185775=CARTESIAN_POINT('Ctrl Pts',(16.6197601561406,18.8850442238484,7.66955339595354));
#185776=CARTESIAN_POINT('Ctrl Pts',(16.8436653936273,17.852883318867,7.60765896285932));
#185777=CARTESIAN_POINT('Ctrl Pts',(18.4531255372358,16.7235436104772,7.50337259420462));
#185778=CARTESIAN_POINT('Ctrl Pts',(20.6735251555922,17.6284160608558,7.3761967875232));
#185779=CARTESIAN_POINT('Ctrl Pts',(21.1145308242001,19.9852110491624,7.24902098084175));
#185780=CARTESIAN_POINT('Ctrl Pts',(19.3715472140107,21.6317154528194,7.12184517416032));
#185781=CARTESIAN_POINT('Ctrl Pts',(17.4471161472743,21.1569083566678,7.0167110424149));
#185782=CARTESIAN_POINT('Ctrl Pts',(16.8648290560492,20.2551146180475,6.95396884622995));
#185783=CARTESIAN_POINT('Ctrl Pts',(16.7486737101886,19.9359290495398,6.93361858560548));
#185784=CARTESIAN_POINT('Ctrl Pts',(16.6170000287534,19.2106510846316,7.68710087888888));
#185785=CARTESIAN_POINT('Ctrl Pts',(16.6169985639082,19.2195388482347,7.68762144435747));
#185786=CARTESIAN_POINT('Ctrl Pts',(16.6170530690843,19.2284264531445,7.68814369819107));
#185787=CARTESIAN_POINT('Ctrl Pts',(16.6172707415968,19.2459375900539,7.68917616888034));
#185788=CARTESIAN_POINT('Ctrl Pts',(16.6174306467683,19.2545609712539,7.6896862739212));
#185789=CARTESIAN_POINT('Ctrl Pts',(16.6177963854112,19.2693940177211,7.69056666315363));
#185790=CARTESIAN_POINT('Ctrl Pts',(16.6179768690834,19.2756042403467,7.69093615259663));
#185791=CARTESIAN_POINT('Ctrl Pts',(16.6183911393839,19.2879820933756,7.69167441523271));
#185792=CARTESIAN_POINT('Ctrl Pts',(16.6186245666227,19.2941496748977,7.69204317358488));
#185793=CARTESIAN_POINT('Ctrl Pts',(16.6191442764776,19.3064570434667,7.69278085951651));
#185794=CARTESIAN_POINT('Ctrl Pts',(16.6194303341968,19.3125967799123,7.69314977649579));
#185795=CARTESIAN_POINT('Ctrl Pts',(16.6202771216571,19.3292146291735,7.69415079514975));
#185796=CARTESIAN_POINT('Ctrl Pts',(16.6208890187398,19.3396898583877,7.69478449629605));
#185797=CARTESIAN_POINT('Ctrl Pts',(16.6234852736182,19.3791005045457,7.69717906122481));
#185798=CARTESIAN_POINT('Ctrl Pts',(16.6259862430463,19.4079976126318,7.69895602824457));
#185799=CARTESIAN_POINT('Ctrl Pts',(16.6474323195092,19.6078897788231,7.71140096947303));
#185800=CARTESIAN_POINT('Ctrl Pts',(16.6865492345595,19.7758840172537,7.7227154079209));
#185801=CARTESIAN_POINT('Ctrl Pts',(16.7454193726886,19.9371102455424,7.73405220823978));
#185802=CARTESIAN_POINT('Origin',(18.734,19.211,0.));
#185803=CARTESIAN_POINT('',(16.7454192421517,19.937109888044,8.75434672885778));
#185804=CARTESIAN_POINT('',(16.7454193934539,19.9371103024118,8.53521106676425));
#185805=CARTESIAN_POINT('',(16.7454193623258,19.9371102171621,0.));
#185806=CARTESIAN_POINT('Ctrl Pts',(16.7454192421517,19.937109888044,8.75434672885778));
#185807=CARTESIAN_POINT('Ctrl Pts',(16.7157810170557,19.8559403500813,8.7495860167213));
#185808=CARTESIAN_POINT('Ctrl Pts',(16.6911130986906,19.7729578545092,8.74492439956724));
#185809=CARTESIAN_POINT('Ctrl Pts',(16.6409703545629,19.5564352327739,8.7328222373515));
#185810=CARTESIAN_POINT('Ctrl Pts',(16.6231411496415,19.4216337344176,8.72532551982903));
#185811=CARTESIAN_POINT('Ctrl Pts',(16.6177334388092,19.2692153742373,8.71640094755641));
#185812=CARTESIAN_POINT('Ctrl Pts',(16.6173369769536,19.2523619417785,8.71540844565238));
#185813=CARTESIAN_POINT('Ctrl Pts',(16.6170471059452,19.2273224546209,8.71392475548325));
#185814=CARTESIAN_POINT('Ctrl Pts',(16.6169998255527,19.2191385925516,8.71343838487837));
#185815=CARTESIAN_POINT('Ctrl Pts',(16.6170001372476,19.20455648059,8.71256911172884));
#185816=CARTESIAN_POINT('Ctrl Pts',(16.6170292805018,19.1981583009378,8.71218679202135));
#185817=CARTESIAN_POINT('Ctrl Pts',(16.6171518843134,19.1846683310924,8.71137874831071));
#185818=CARTESIAN_POINT('Ctrl Pts',(16.6172519794828,19.1775766936962,8.71095282096323));
#185819=CARTESIAN_POINT('Ctrl Pts',(16.6176113756871,19.1588005197579,8.70982203094684));
#185820=CARTESIAN_POINT('Ctrl Pts',(16.6179318028125,19.1471175209732,8.70911526177061));
#185821=CARTESIAN_POINT('Ctrl Pts',(16.6198779961695,19.092626327482,8.70580361777299));
#185822=CARTESIAN_POINT('Ctrl Pts',(16.6227060712719,19.0498736487773,8.70316137440709));
#185823=CARTESIAN_POINT('Ctrl Pts',(16.6340979484588,18.932066147754,8.69575359139213));
#185824=CARTESIAN_POINT('Ctrl Pts',(16.6453836934642,18.8573438162893,8.69090977847032));
#185825=CARTESIAN_POINT('Ctrl Pts',(16.6865619342682,18.6576816958607,8.67762193719792));
#185826=CARTESIAN_POINT('Ctrl Pts',(16.7238651788393,18.534597802203,8.66904374240272));
#185827=CARTESIAN_POINT('Ctrl Pts',(16.7783252999815,18.4002587320868,8.65959211326805));
#185828=CARTESIAN_POINT('Ctrl Pts',(16.7847471862453,18.3849380020785,8.6585131872796));
#185829=CARTESIAN_POINT('Ctrl Pts',(16.8125068533598,18.3208384232824,8.65399898077157));
#185830=CARTESIAN_POINT('Ctrl Pts',(16.835502363072,18.2727935733103,8.65061472031495));
#185831=CARTESIAN_POINT('Ctrl Pts',(16.8643428399077,18.2179506392627,8.64679236635273));
#185832=CARTESIAN_POINT('Ctrl Pts',(16.8684462209151,18.2102632551545,8.64625754915743));
#185833=CARTESIAN_POINT('Ctrl Pts',(16.8747318686502,18.1986605794638,8.64545206171907));
#185834=CARTESIAN_POINT('Ctrl Pts',(16.8768792380025,18.1947266298691,8.64517925828317));
#185835=CARTESIAN_POINT('Ctrl Pts',(16.8807565432377,18.1876767906512,8.64469096367063));
#185836=CARTESIAN_POINT('Ctrl Pts',(16.8824818607172,18.1845584374576,8.64447518482431));
#185837=CARTESIAN_POINT('Ctrl Pts',(16.8862483287793,18.1777912889107,8.64400738000286));
#185838=CARTESIAN_POINT('Ctrl Pts',(16.888292409414,18.1741441903925,8.64375554540963));
#185839=CARTESIAN_POINT('Ctrl Pts',(16.8940655214934,18.1639148336062,8.64304993504256));
#185840=CARTESIAN_POINT('Ctrl Pts',(16.8978190937605,18.1573463973602,8.64259770746247));
#185841=CARTESIAN_POINT('Ctrl Pts',(16.920491720224,18.1181603300801,8.63990408020139));
#185842=CARTESIAN_POINT('Ctrl Pts',(16.9402455404157,18.0860305961332,8.63771329206219));
#185843=CARTESIAN_POINT('Ctrl Pts',(17.0081342721693,17.9819483347955,8.6306175892307));
#185844=CARTESIAN_POINT('Ctrl Pts',(17.0598254413951,17.9124152229069,8.62587709572191));
#185845=CARTESIAN_POINT('Ctrl Pts',(17.2291734117859,17.7115983654371,8.61158244377948));
#185846=CARTESIAN_POINT('Ctrl Pts',(17.359056748435,17.5916690556861,8.60211687411541));
#185847=CARTESIAN_POINT('Ctrl Pts',(17.5209475325225,17.4758575769542,8.59054984392107));
#185848=CARTESIAN_POINT('Ctrl Pts',(17.5398251272281,17.4628118437123,8.58920550140768));
#185849=CARTESIAN_POINT('Ctrl Pts',(17.5668448509374,17.4447812011437,8.58728581481007));
#185850=CARTESIAN_POINT('Ctrl Pts',(17.5748147779222,17.4395402618726,8.58672011599731));
#185851=CARTESIAN_POINT('Ctrl Pts',(17.5878261804781,17.4311095082105,8.58579734116235));
#185852=CARTESIAN_POINT('Ctrl Pts',(17.5928462560111,17.4278867902518,8.58544149819128));
#185853=CARTESIAN_POINT('Ctrl Pts',(17.6033863121168,17.4211831727129,8.58469472588016));
#185854=CARTESIAN_POINT('Ctrl Pts',(17.608908893192,17.4177064974271,8.58430364495242));
#185855=CARTESIAN_POINT('Ctrl Pts',(17.6220914791847,17.4094924203722,8.58337054817236));
#185856=CARTESIAN_POINT('Ctrl Pts',(17.6297657685229,17.4047782870772,8.58282768260985));
#185857=CARTESIAN_POINT('Ctrl Pts',(17.6557517782801,17.3890432085181,8.58099047340844));
#185858=CARTESIAN_POINT('Ctrl Pts',(17.6741997808944,17.3782509116931,8.57968783918529));
#185859=CARTESIAN_POINT('Ctrl Pts',(17.7757285137036,17.3209009128484,8.57252536000152));
#185860=CARTESIAN_POINT('Ctrl Pts',(17.861704493767,17.279716716662,8.56647648154496));
#185861=CARTESIAN_POINT('Ctrl Pts',(18.1086082070268,17.1813024573805,8.54920487185127));
#185862=CARTESIAN_POINT('Ctrl Pts',(18.2741081412925,17.137528675116,8.53769527547674));
#185863=CARTESIAN_POINT('Ctrl Pts',(18.4795040648143,17.109030822944,8.52446033264503));
#185864=CARTESIAN_POINT('Ctrl Pts',(18.516074543654,17.1049251022296,8.52214603687204));
#185865=CARTESIAN_POINT('Ctrl Pts',(18.5598517151202,17.1011629484618,8.51944028791996));
#185866=CARTESIAN_POINT('Ctrl Pts',(18.5669707224031,17.1005874259013,8.51900231736309));
#185867=CARTESIAN_POINT('Ctrl Pts',(18.5785921108759,17.0997070905289,8.51829082567716));
#185868=CARTESIAN_POINT('Ctrl Pts',(18.5830927276043,17.0993806314596,8.51801613495573));
#185869=CARTESIAN_POINT('Ctrl Pts',(18.5911518306737,17.0988219495888,8.51752581653014));
#185870=CARTESIAN_POINT('Ctrl Pts',(18.5947098785228,17.0985843262311,8.51730989063227));
#185871=CARTESIAN_POINT('Ctrl Pts',(18.602417861842,17.0980891101583,8.51684330903261));
#185872=CARTESIAN_POINT('Ctrl Pts',(18.6065679477215,17.0978347532129,8.51659283640032));
#185873=CARTESIAN_POINT('Ctrl Pts',(18.6181656265467,17.097158226854,8.5158948791704));
#185874=CARTESIAN_POINT('Ctrl Pts',(18.6256148258465,17.0967631869273,8.51544888925012));
#185875=CARTESIAN_POINT('Ctrl Pts',(18.6689433369407,17.0946950265628,8.51286739279311));
#185876=CARTESIAN_POINT('Ctrl Pts',(18.7048607989835,17.0938957600832,8.51077771975786));
#185877=CARTESIAN_POINT('Ctrl Pts',(18.8205156815905,17.0942663562862,8.50416137048909));
#185878=CARTESIAN_POINT('Ctrl Pts',(18.9001762731438,17.0990261098268,8.4997747462917));
#185879=CARTESIAN_POINT('Ctrl Pts',(19.1643338362318,17.1298526834424,8.48527478373422));
#185880=CARTESIAN_POINT('Ctrl Pts',(19.345606585014,17.1757376606257,8.47531866330219));
#185881=CARTESIAN_POINT('Ctrl Pts',(19.5390168233056,17.2529083166128,8.46320680919834));
#185882=CARTESIAN_POINT('Ctrl Pts',(19.5593656917881,17.2613983618914,8.46191427765178));
#185883=CARTESIAN_POINT('Ctrl Pts',(19.5873241350491,17.2735794678152,8.4601115200669));
#185884=CARTESIAN_POINT('Ctrl Pts',(19.5950502078706,17.2770007925624,8.45961047305527));
#185885=CARTESIAN_POINT('Ctrl Pts',(19.6082959568594,17.2829614908691,8.45874643214269));
#185886=CARTESIAN_POINT('Ctrl Pts',(19.613825602712,17.2854785588051,8.45838420642187));
#185887=CARTESIAN_POINT('Ctrl Pts',(19.6252035291611,17.2907169798876,8.45763571096));
#185888=CARTESIAN_POINT('Ctrl Pts',(19.6310503546376,17.2934413261813,8.45724934083109));
#185889=CARTESIAN_POINT('Ctrl Pts',(19.6446284388797,17.2998437671049,8.4563479781304));
#185890=CARTESIAN_POINT('Ctrl Pts',(19.6523499770234,17.3035421062137,8.4558322873104));
#185891=CARTESIAN_POINT('Ctrl Pts',(19.6769967860088,17.3155313866904,8.4541761279058));
#185892=CARTESIAN_POINT('Ctrl Pts',(19.6938334934141,17.3240013695471,8.45302943476264));
#185893=CARTESIAN_POINT('Ctrl Pts',(19.7773918526518,17.3674444097246,8.44725987905308));
#185894=CARTESIAN_POINT('Ctrl Pts',(19.8423195681874,17.4057328901836,8.44252062808619));
#185895=CARTESIAN_POINT('Ctrl Pts',(19.9960048664068,17.5077825723649,8.43066534842997));
#185896=CARTESIAN_POINT('Ctrl Pts',(20.0821329796339,17.5751088404482,8.42344948268122));
#185897=CARTESIAN_POINT('Ctrl Pts',(20.1730469185298,17.6582507056954,8.4153109194896));
#185898=CARTESIAN_POINT('Ctrl Pts',(20.1833205019861,17.6678355596029,8.41438324490779));
#185899=CARTESIAN_POINT('Ctrl Pts',(20.2693745607069,17.7497380859648,8.40654865238302));
#185900=CARTESIAN_POINT('Ctrl Pts',(20.3397961775604,17.8274952925357,8.39970425921115));
#185901=CARTESIAN_POINT('Ctrl Pts',(20.4101292728072,17.9177971998412,8.39263247832015));
#185902=CARTESIAN_POINT('Ctrl Pts',(20.4160287886,17.9254798780245,8.39203733616778));
#185903=CARTESIAN_POINT('Ctrl Pts',(20.4246627373285,17.9368846863119,8.39116375664565));
#185904=CARTESIAN_POINT('Ctrl Pts',(20.4274379581797,17.9405755800935,8.39088255902664));
#185905=CARTESIAN_POINT('Ctrl Pts',(20.43234052854,17.9471403427675,8.39038513719908));
#185906=CARTESIAN_POINT('Ctrl Pts',(20.4344726942659,17.9500105469131,8.39016857867322));
#185907=CARTESIAN_POINT('Ctrl Pts',(20.4390259579952,17.9561724505841,8.3897056394285));
#185908=CARTESIAN_POINT('Ctrl Pts',(20.4414447939497,17.9594657525763,8.38945941528889));
#185909=CARTESIAN_POINT('Ctrl Pts',(20.4480596526018,17.9685269092461,8.38878518002722));
#185910=CARTESIAN_POINT('Ctrl Pts',(20.4522361292553,17.9743090598927,8.38835850311727));
#185911=CARTESIAN_POINT('Ctrl Pts',(20.4743984684497,18.0053208609879,8.38608843904006));
#185912=CARTESIAN_POINT('Ctrl Pts',(20.4918590539263,18.030923396526,8.3842789219611));
#185913=CARTESIAN_POINT('Ctrl Pts',(20.5979130315293,18.1940113308806,8.37308987090836));
#185914=CARTESIAN_POINT('Ctrl Pts',(20.6708945644685,18.3410060131363,8.36444575549577));
#185915=CARTESIAN_POINT('Ctrl Pts',(20.7660370281603,18.6057165134807,8.34905100060105));
#185916=CARTESIAN_POINT('Ctrl Pts',(20.7965363340944,18.7195927261857,8.34248309119627));
#185917=CARTESIAN_POINT('Ctrl Pts',(20.8199519706694,18.8494783661356,8.33475140450648));
#185918=CARTESIAN_POINT('Ctrl Pts',(20.8223464956857,18.8635774694906,8.33390925781615));
#185919=CARTESIAN_POINT('Ctrl Pts',(20.825929558127,18.8860519121019,8.33256184678198));
#185920=CARTESIAN_POINT('Ctrl Pts',(20.8272110876084,18.8944121361446,8.33205952938785));
#185921=CARTESIAN_POINT('Ctrl Pts',(20.8293826154467,18.9091682715513,8.33117089933053));
#185922=CARTESIAN_POINT('Ctrl Pts',(20.8302935176405,18.9155610318745,8.33078525374142));
#185923=CARTESIAN_POINT('Ctrl Pts',(20.8321168089426,18.9287901080542,8.32998578581025));
#185924=CARTESIAN_POINT('Ctrl Pts',(20.8330250654306,18.935626907592,8.32957183765141));
#185925=CARTESIAN_POINT('Ctrl Pts',(20.8352702089983,18.9531837575925,8.32850675969558));
#185926=CARTESIAN_POINT('Ctrl Pts',(20.8365584644048,18.963909726905,8.32785410279159));
#185927=CARTESIAN_POINT('Ctrl Pts',(20.8415891915576,19.0086875503363,8.32512093933148));
#185928=CARTESIAN_POINT('Ctrl Pts',(20.8445867801644,19.042816303812,8.32301716319151));
#185929=CARTESIAN_POINT('Ctrl Pts',(20.8502361087326,19.1318891338896,8.31746970197765));
#185930=CARTESIAN_POINT('Ctrl Pts',(20.8515768176137,19.1868877189968,8.31398775225973));
#185931=CARTESIAN_POINT('Ctrl Pts',(20.8491808393078,19.3511675712616,8.30342808394179));
#185932=CARTESIAN_POINT('Ctrl Pts',(20.8391244680064,19.4601674877784,8.29620194200463));
#185933=CARTESIAN_POINT('Ctrl Pts',(20.8141428443948,19.6062308953486,8.28641310355518));
#185934=CARTESIAN_POINT('Ctrl Pts',(20.8065306075094,19.644380549066,8.28384781553478));
#185935=CARTESIAN_POINT('Ctrl Pts',(20.7916044183325,19.7097439602419,8.27945625055897));
#185936=CARTESIAN_POINT('Ctrl Pts',(20.784790282331,19.7370615832903,8.27762202758441));
#185937=CARTESIAN_POINT('Ctrl Pts',(20.7636571585287,19.8151189270608,8.27239776714489));
#185938=CARTESIAN_POINT('Ctrl Pts',(20.7479841263705,19.8654744474717,8.26904797779021));
#185939=CARTESIAN_POINT('Ctrl Pts',(20.7275548222699,19.9233929477802,8.26525958796411));
#185940=CARTESIAN_POINT('Ctrl Pts',(20.7246131989483,19.9315717449132,8.26472615454234));
#185941=CARTESIAN_POINT('Ctrl Pts',(20.7200801154302,19.9439357534643,8.26392233435536));
#185942=CARTESIAN_POINT('Ctrl Pts',(20.718525653361,19.9481342995805,8.26364982731118));
#185943=CARTESIAN_POINT('Ctrl Pts',(20.7157100019476,19.9556658088046,8.26316184887843));
#185944=CARTESIAN_POINT('Ctrl Pts',(20.7144537117193,19.9590005313757,8.26294609147541));
#185945=CARTESIAN_POINT('Ctrl Pts',(20.7117038744118,19.9662442620297,8.26247808702039));
#185946=CARTESIAN_POINT('Ctrl Pts',(20.7102071607625,19.9701520062799,8.26222603268439));
#185947=CARTESIAN_POINT('Ctrl Pts',(20.7059659163146,19.9811278559652,8.26151918508505));
#185948=CARTESIAN_POINT('Ctrl Pts',(20.7031949538382,19.9881857740329,8.26106594874796));
#185949=CARTESIAN_POINT('Ctrl Pts',(20.6863067963199,20.0305313740432,8.25835358695102));
#185950=CARTESIAN_POINT('Ctrl Pts',(20.6712783760478,20.0654509339158,8.25614589577525));
#185951=CARTESIAN_POINT('Ctrl Pts',(20.6184747587762,20.1795772223817,8.24896765860186));
#185952=CARTESIAN_POINT('Ctrl Pts',(20.5767150514121,20.2568444580941,8.24416593257567));
#185953=CARTESIAN_POINT('Ctrl Pts',(20.4379674414183,20.4793105260659,8.22990246545836));
#185954=CARTESIAN_POINT('Ctrl Pts',(20.3277314422174,20.6153254519113,8.22051951224964));
#185955=CARTESIAN_POINT('Ctrl Pts',(20.1854463175807,20.7522737337603,8.20904488838432));
#185956=CARTESIAN_POINT('Ctrl Pts',(20.1685661699803,20.7679974237718,8.20769350237637));
#185957=CARTESIAN_POINT('Ctrl Pts',(20.1443329418042,20.789841779301,8.20576548130794));
#185958=CARTESIAN_POINT('Ctrl Pts',(20.1371897818766,20.7961936166559,8.20519860740392));
#185959=CARTESIAN_POINT('Ctrl Pts',(20.1255165097517,20.8064329925923,8.20427443936026));
#185960=CARTESIAN_POINT('Ctrl Pts',(20.1210124899567,20.8103501750223,8.20391838580633));
#185961=CARTESIAN_POINT('Ctrl Pts',(20.1115522492655,20.8185078057948,8.20317159790929));
#185962=CARTESIAN_POINT('Ctrl Pts',(20.106592883472,20.8227444958528,8.20278071386163));
#185963=CARTESIAN_POINT('Ctrl Pts',(20.094752451206,20.8327652637287,8.20184887360752));
#185964=CARTESIAN_POINT('Ctrl Pts',(20.087854009665,20.8385285314606,8.20130707372926));
#185965=CARTESIAN_POINT('Ctrl Pts',(20.0645100910978,20.8577799729748,8.19947721279945));
#185966=CARTESIAN_POINT('Ctrl Pts',(20.047898515629,20.8710638604358,8.19818095107264));
#185967=CARTESIAN_POINT('Ctrl Pts',(19.9091770816075,20.9786095840789,8.18740045945979));
#185968=CARTESIAN_POINT('Ctrl Pts',(19.7773214391571,21.0594990095322,8.17738215137559));
#185969=CARTESIAN_POINT('Ctrl Pts',(19.5140008039101,21.1838290699065,8.15815538318633));
#185970=CARTESIAN_POINT('Ctrl Pts',(19.3847282058745,21.230161927364,8.149040620382));
#185971=CARTESIAN_POINT('Ctrl Pts',(19.2367732322497,21.2674898967102,8.13952316503127));
#185972=CARTESIAN_POINT('Ctrl Pts',(19.221628164573,21.2711335937323,8.13855954269121));
#185973=CARTESIAN_POINT('Ctrl Pts',(19.2008163662,21.2758982560037,8.13725116375012));
#185974=CARTESIAN_POINT('Ctrl Pts',(19.1951836479804,21.277163587916,8.13689862968871));
#185975=CARTESIAN_POINT('Ctrl Pts',(19.1862178913223,21.279139161446,8.13634007765771));
#185976=CARTESIAN_POINT('Ctrl Pts',(19.1828882407298,21.2798644131634,8.13613321199359));
#185977=CARTESIAN_POINT('Ctrl Pts',(19.1760021450707,21.281346909377,8.13570658079827));
#185978=CARTESIAN_POINT('Ctrl Pts',(19.1724454975944,21.2821030315286,8.13548688568062));
#185979=CARTESIAN_POINT('Ctrl Pts',(19.1639566851621,21.2838848561474,8.13496406611253));
#185980=CARTESIAN_POINT('Ctrl Pts',(19.1590227345578,21.2849021322771,8.13466142250815));
#185981=CARTESIAN_POINT('Ctrl Pts',(19.1423270045487,21.2882823539886,8.13364135135323));
#185982=CARTESIAN_POINT('Ctrl Pts',(19.1305485375182,21.290562981309,8.13292846449497));
#185983=CARTESIAN_POINT('Ctrl Pts',(18.9927709103271,21.3160272539301,8.12466153894752));
#185984=CARTESIAN_POINT('Ctrl Pts',(18.8649180334723,21.3278306590802,8.1176828596066));
#185985=CARTESIAN_POINT('Ctrl Pts',(18.5726319299503,21.3282127664952,8.1018012615305));
#185986=CARTESIAN_POINT('Ctrl Pts',(18.4090489091375,21.3093396780551,8.09292709736246));
#185987=CARTESIAN_POINT('Ctrl Pts',(18.2260731696542,21.2663024989553,8.08201387484432));
#185988=CARTESIAN_POINT('Ctrl Pts',(18.2029472457859,21.2604489336314,8.08061716088213));
#185989=CARTESIAN_POINT('Ctrl Pts',(18.1705739508108,21.2516699822171,8.07863539286552));
#185990=CARTESIAN_POINT('Ctrl Pts',(18.1612397076422,21.2490698054735,8.07806086093737));
#185991=CARTESIAN_POINT('Ctrl Pts',(18.1461616475604,21.2447578490723,8.07712759892786));
#185992=CARTESIAN_POINT('Ctrl Pts',(18.1404066046115,21.2430855781871,8.07677015889863));
#185993=CARTESIAN_POINT('Ctrl Pts',(18.1284216801365,21.2395478031464,8.07602318628565));
#185994=CARTESIAN_POINT('Ctrl Pts',(18.1221931463947,21.2376779871395,8.07563351600594));
#185995=CARTESIAN_POINT('Ctrl Pts',(18.1074804407252,21.2331872049731,8.07470952997878));
#185996=CARTESIAN_POINT('Ctrl Pts',(18.0990039985633,21.230541513442,8.07417440820428));
#185997=CARTESIAN_POINT('Ctrl Pts',(18.0714817365435,21.221760783892,8.07242770000741));
#185998=CARTESIAN_POINT('Ctrl Pts',(18.0525066426356,21.2154091748382,8.07120901669527));
#185999=CARTESIAN_POINT('Ctrl Pts',(18.0077194297273,21.1997078990107,8.06829733983408));
#186000=CARTESIAN_POINT('Ctrl Pts',(17.9819940261754,21.1901234120518,8.06659680007746));
#186001=CARTESIAN_POINT('Ctrl Pts',(17.7996873526842,21.1181340019909,8.05434117138343));
#186002=CARTESIAN_POINT('Ctrl Pts',(17.6508872590648,21.0377318146349,8.04317898634587));
#186003=CARTESIAN_POINT('Ctrl Pts',(17.4270801356029,20.879762041665,8.02511096216918));
#186004=CARTESIAN_POINT('Ctrl Pts',(17.3455900609167,20.8126021379574,8.01821923985443));
#186005=CARTESIAN_POINT('Ctrl Pts',(17.2624433137892,20.732940776907,8.01110491570271));
#186006=CARTESIAN_POINT('Ctrl Pts',(17.2554955209156,20.7261921735057,8.01050981322381));
#186007=CARTESIAN_POINT('Ctrl Pts',(17.245303980766,20.7161559670475,8.00963628060322));
#186008=CARTESIAN_POINT('Ctrl Pts',(17.2420243956032,20.7129051633307,8.00935509063059));
#186009=CARTESIAN_POINT('Ctrl Pts',(17.2362243313436,20.7071182541331,8.00885767725378));
#186010=CARTESIAN_POINT('Ctrl Pts',(17.233699616995,20.7045864706815,8.00864111957486));
#186011=CARTESIAN_POINT('Ctrl Pts',(17.2283032898717,20.699147544418,8.00817817652515));
#186012=CARTESIAN_POINT('Ctrl Pts',(17.2254336840742,20.6962384885776,8.00793194776295));
#186013=CARTESIAN_POINT('Ctrl Pts',(17.2195619304922,20.6902514390753,8.00742796899478));
#186014=CARTESIAN_POINT('Ctrl Pts',(17.2165606987033,20.6871725691774,8.00717028984034));
#186015=CARTESIAN_POINT('Ctrl Pts',(17.2028029611228,20.6729726422423,8.00598858882848));
#186016=CARTESIAN_POINT('Ctrl Pts',(17.1921588701945,20.6617426857487,8.00507294015027));
#186017=CARTESIAN_POINT('Ctrl Pts',(17.1270483444767,20.5915222426383,7.99945554326263));
#186018=CARTESIAN_POINT('Ctrl Pts',(17.0758455863945,20.5295833190372,7.99496505990111));
#186019=CARTESIAN_POINT('Ctrl Pts',(16.9870774679686,20.4088272838093,7.98672570890619));
#186020=CARTESIAN_POINT('Ctrl Pts',(16.9486608446298,20.3507776227368,7.98296292502071));
#186021=CARTESIAN_POINT('Ctrl Pts',(16.8464151207174,20.1783867715229,7.97206976135757));
#186022=CARTESIAN_POINT('Ctrl Pts',(16.790267739069,20.059935407336,7.96490130145217));
#186023=CARTESIAN_POINT('Ctrl Pts',(16.7454193311435,19.9371101317641,7.95734462820299));
#186024=CARTESIAN_POINT('Ctrl Pts',(16.7454193726886,19.9371102455424,7.73405220823978));
#186025=CARTESIAN_POINT('Ctrl Pts',(16.7614416071399,19.9809899528345,7.73713765832381));
#186026=CARTESIAN_POINT('Ctrl Pts',(16.7789269230783,20.0243687437115,7.74021945161001));
#186027=CARTESIAN_POINT('Ctrl Pts',(16.8241807251844,20.1267054853234,7.74752070944097));
#186028=CARTESIAN_POINT('Ctrl Pts',(16.853240883593,20.1849984452125,7.75170524900241));
#186029=CARTESIAN_POINT('Ctrl Pts',(16.8913431829543,20.2533423367608,7.75656672675373));
#186030=CARTESIAN_POINT('Ctrl Pts',(16.8978491813239,20.2647608283762,7.75737736942318));
#186031=CARTESIAN_POINT('Ctrl Pts',(16.9070905289816,20.2806345610226,7.75850128692437));
#186032=CARTESIAN_POINT('Ctrl Pts',(16.90973653366,20.2851411062559,7.75882002295505));
#186033=CARTESIAN_POINT('Ctrl Pts',(16.9142695216255,20.2927964043434,7.75936081404305));
#186034=CARTESIAN_POINT('Ctrl Pts',(16.9161480474682,20.2959501158012,7.75958341237253));
#186035=CARTESIAN_POINT('Ctrl Pts',(16.9197628321593,20.3019829523373,7.7600088436105));
#186036=CARTESIAN_POINT('Ctrl Pts',(16.921497752063,20.30486283649,7.76021176434571));
#186037=CARTESIAN_POINT('Ctrl Pts',(16.9261081646349,20.3124748169595,7.76074770715533));
#186038=CARTESIAN_POINT('Ctrl Pts',(16.9289953978466,20.3171998230673,7.76107996558489));
#186039=CARTESIAN_POINT('Ctrl Pts',(16.9392862663533,20.3338934377739,7.76225255944951));
#186040=CARTESIAN_POINT('Ctrl Pts',(16.9467908570666,20.3457997891742,7.763086533279));
#186041=CARTESIAN_POINT('Ctrl Pts',(17.0425700446124,20.4944503576821,7.77348057342281));
#186042=CARTESIAN_POINT('Ctrl Pts',(17.1462244454709,20.620668471612,7.78214130874963));
#186043=CARTESIAN_POINT('Ctrl Pts',(17.3537662764628,20.8211084582887,7.79784826975427));
#186044=CARTESIAN_POINT('Ctrl Pts',(17.4517854744826,20.9002054247221,7.8047787964754));
#186045=CARTESIAN_POINT('Ctrl Pts',(17.5701088041064,20.9794244492968,7.81304298815136));
#186046=CARTESIAN_POINT('Ctrl Pts',(17.5840913685183,20.9885482735955,7.8140177319333));
#186047=CARTESIAN_POINT('Ctrl Pts',(17.606402319916,21.0027330725957,7.81557093431809));
#186048=CARTESIAN_POINT('Ctrl Pts',(17.6146604205226,21.0079036792868,7.81614537631878));
#186049=CARTESIAN_POINT('Ctrl Pts',(17.6303732837561,21.0175915548133,7.81723768368851));
#186050=CARTESIAN_POINT('Ctrl Pts',(17.6378208442782,21.0221201588599,7.81775512124974));
#186051=CARTESIAN_POINT('Ctrl Pts',(17.6507774341252,21.0298894197626,7.81865490164893));
#186052=CARTESIAN_POINT('Ctrl Pts',(17.656273602304,21.0331513819856,7.81903646029143));
#186053=CARTESIAN_POINT('Ctrl Pts',(17.6669320886513,21.039412074421,7.81977619336423));
#186054=CARTESIAN_POINT('Ctrl Pts',(17.6720924917106,21.042413957581,7.82013424849662));
#186055=CARTESIAN_POINT('Ctrl Pts',(17.6855524729191,21.0501678137,7.82106796577067));
#186056=CARTESIAN_POINT('Ctrl Pts',(17.6938716086648,21.0548854055596,7.8216448619957));
#186057=CARTESIAN_POINT('Ctrl Pts',(17.7223434748233,21.0707771548432,7.8236187549177));
#186058=CARTESIAN_POINT('Ctrl Pts',(17.7426459997752,21.0816782649608,7.82502544470214));
#186059=CARTESIAN_POINT('Ctrl Pts',(17.9182807179758,21.1723202994331,7.83719163970475));
#186060=CARTESIAN_POINT('Ctrl Pts',(18.0827223620787,21.232877742226,7.84864683896861));
#186061=CARTESIAN_POINT('Ctrl Pts',(18.3380271012821,21.2924836278559,7.86596942371986));
#186062=CARTESIAN_POINT('Ctrl Pts',(18.4245259748775,21.3070907399696,7.87174652517322));
#186063=CARTESIAN_POINT('Ctrl Pts',(18.5494557209725,21.3202830242743,7.879768160808));
#186064=CARTESIAN_POINT('Ctrl Pts',(18.5873288471997,21.3232545905153,7.88215744255913));
#186065=CARTESIAN_POINT('Ctrl Pts',(18.6328346665505,21.3255950066018,7.88496142987693));
#186066=CARTESIAN_POINT('Ctrl Pts',(18.640407504597,21.3259437144835,7.8854258366451));
#186067=CARTESIAN_POINT('Ctrl Pts',(18.6521629158985,21.3264217544263,7.88614312887025));
#186068=CARTESIAN_POINT('Ctrl Pts',(18.6563441858421,21.3265793728105,7.8863975528922));
#186069=CARTESIAN_POINT('Ctrl Pts',(18.664087355159,21.3268482745901,7.8868673661047));
#186070=CARTESIAN_POINT('Ctrl Pts',(18.667649037583,21.3269629602339,7.88708293814638));
#186071=CARTESIAN_POINT('Ctrl Pts',(18.6756865398418,21.3272014525484,7.88756822366703));
#186072=CARTESIAN_POINT('Ctrl Pts',(18.6801624600447,21.3273200531919,7.88783764298509));
#186073=CARTESIAN_POINT('Ctrl Pts',(18.6933298308605,21.3276271549256,7.88862788478297));
#186074=CARTESIAN_POINT('Ctrl Pts',(18.7020222265683,21.3277763234453,7.889146558561));
#186075=CARTESIAN_POINT('Ctrl Pts',(18.7635129971128,21.3284526913115,7.89279601711676));
#186076=CARTESIAN_POINT('Ctrl Pts',(18.8163185965995,21.3270580231469,7.895827496855));
#186077=CARTESIAN_POINT('Ctrl Pts',(18.885088170904,21.3226629860662,7.89970463401846));
#186078=CARTESIAN_POINT('Ctrl Pts',(18.9011432035323,21.3214528827362,7.90060472921187));
#186079=CARTESIAN_POINT('Ctrl Pts',(18.9674699475352,21.3156920492803,7.90430771357342));
#186080=CARTESIAN_POINT('Ctrl Pts',(19.0175861870824,21.3095271149566,7.90706908851281));
#186081=CARTESIAN_POINT('Ctrl Pts',(19.1754742620877,21.2843448232093,7.9157741024952));
#186082=CARTESIAN_POINT('Ctrl Pts',(19.2820135694758,21.2587642760604,7.92166485657649));
#186083=CARTESIAN_POINT('Ctrl Pts',(19.4385873721785,21.2080703528659,7.9308153865112));
#186084=CARTESIAN_POINT('Ctrl Pts',(19.4903925911689,21.1890300705561,7.93392645348369));
#186085=CARTESIAN_POINT('Ctrl Pts',(19.5731344739018,21.1548933578749,7.93907581755766));
#186086=CARTESIAN_POINT('Ctrl Pts',(19.604551705176,21.1410278711995,7.94107461940823));
#186087=CARTESIAN_POINT('Ctrl Pts',(19.645399306145,21.121800149435,7.94373719886824));
#186088=CARTESIAN_POINT('Ctrl Pts',(19.655146444088,21.1171204390861,7.94437740450623));
#186089=CARTESIAN_POINT('Ctrl Pts',(19.6710533820928,21.1093328354737,7.94543035561458));
#186090=CARTESIAN_POINT('Ctrl Pts',(19.6772346703264,21.1062690970126,7.94584155839544));
#186091=CARTESIAN_POINT('Ctrl Pts',(19.6891716657971,21.1002796975685,7.94663965177085));
#186092=CARTESIAN_POINT('Ctrl Pts',(19.6949291877685,21.0973578084362,7.94702640667253));
#186093=CARTESIAN_POINT('Ctrl Pts',(19.7081933950114,21.090549861102,7.94792165549318));
#186094=CARTESIAN_POINT('Ctrl Pts',(19.7156903140597,21.0866451091015,7.94843080494301));
#186095=CARTESIAN_POINT('Ctrl Pts',(19.735792086032,21.076021618663,7.94980461916907));
#186096=CARTESIAN_POINT('Ctrl Pts',(19.7483524897321,21.0692201249031,7.95067220873737));
#186097=CARTESIAN_POINT('Ctrl Pts',(19.8612905143558,21.0065776060221,7.95855788522971));
#186098=CARTESIAN_POINT('Ctrl Pts',(19.9570208788332,20.9427896348113,7.96586707868778));
#186099=CARTESIAN_POINT('Ctrl Pts',(20.0998234888755,20.829868139343,7.97775017929054));
#186100=CARTESIAN_POINT('Ctrl Pts',(20.1505349486765,20.785686016252,7.9821913832998));
#186101=CARTESIAN_POINT('Ctrl Pts',(20.2643817514613,20.6765409158214,7.99261347857898));
#186102=CARTESIAN_POINT('Ctrl Pts',(20.3256277748713,20.6097857258951,7.99858644373108));
#186103=CARTESIAN_POINT('Ctrl Pts',(20.4066929445638,20.5091850042919,8.00684123117954));
#186104=CARTESIAN_POINT('Ctrl Pts',(20.4301409572904,20.4783958662819,8.00927639645246));
#186105=CARTESIAN_POINT('Ctrl Pts',(20.4571825945517,20.4407921855456,8.01212684999798));
#186106=CARTESIAN_POINT('Ctrl Pts',(20.4615984173786,20.4345811318094,8.01259373250377));
#186107=CARTESIAN_POINT('Ctrl Pts',(20.4683917108544,20.4249159663279,8.01331401534913));
#186108=CARTESIAN_POINT('Ctrl Pts',(20.4707925684088,20.421478481845,8.01356897445338));
#186109=CARTESIAN_POINT('Ctrl Pts',(20.475214640622,20.4151068347051,8.01403928436898));
#186110=CARTESIAN_POINT('Ctrl Pts',(20.4772386440805,20.4121747267545,8.01425482117396));
#186111=CARTESIAN_POINT('Ctrl Pts',(20.4817832703416,20.4055553935235,8.01473941048924));
#186112=CARTESIAN_POINT('Ctrl Pts',(20.4842996249741,20.4018653038604,8.01500817258838));
#186113=CARTESIAN_POINT('Ctrl Pts',(20.4916506071043,20.3910118767057,8.01579470321554));
#186114=CARTESIAN_POINT('Ctrl Pts',(20.4964531385041,20.3838267673338,8.01631035316076));
#186115=CARTESIAN_POINT('Ctrl Pts',(20.5295917244417,20.3335845952032,8.01988256980961));
#186116=CARTESIAN_POINT('Ctrl Pts',(20.5563934477622,20.2895308826218,8.02284455661355));
#186117=CARTESIAN_POINT('Ctrl Pts',(20.5884267037649,20.2322679851554,8.02654016216896));
#186118=CARTESIAN_POINT('Ctrl Pts',(20.595168852791,20.2199287444364,8.02732765445513));
#186119=CARTESIAN_POINT('Ctrl Pts',(20.6769258886446,20.0666911618065,8.03700947129375));
#186120=CARTESIAN_POINT('Ctrl Pts',(20.7358971234608,19.9178104785668,8.0454408790572));
#186121=CARTESIAN_POINT('Ctrl Pts',(20.7981774096809,19.6875368405104,8.05867901546202));
#186122=CARTESIAN_POINT('Ctrl Pts',(20.8145023666282,19.6102789790718,8.06314414533086));
#186123=CARTESIAN_POINT('Ctrl Pts',(20.8294094735106,19.5131946144835,8.06887605107643));
#186124=CARTESIAN_POINT('Ctrl Pts',(20.8320806267839,19.4940549303999,8.0700116466015));
#186125=CARTESIAN_POINT('Ctrl Pts',(20.8355673653284,19.4663006228896,8.07166744477738));
#186126=CARTESIAN_POINT('Ctrl Pts',(20.8365928017403,19.4577130027913,8.07218102705942));
#186127=CARTESIAN_POINT('Ctrl Pts',(20.838292664879,19.442696279926,8.07308138094401));
#186128=CARTESIAN_POINT('Ctrl Pts',(20.8389903239764,19.4362698828748,8.07346741491033));
#186129=CARTESIAN_POINT('Ctrl Pts',(20.8402840342536,19.4238219458645,8.07421661052226));
#186130=CARTESIAN_POINT('Ctrl Pts',(20.8408837235466,19.4178008410659,8.07457965348905));
#186131=CARTESIAN_POINT('Ctrl Pts',(20.842250039493,19.4034593146041,8.07544597038146));
#186132=CARTESIAN_POINT('Ctrl Pts',(20.8429932311686,19.3951368093399,8.07594997711387));
#186133=CARTESIAN_POINT('Ctrl Pts',(20.8454697078749,19.3654195882152,8.07775431039218));
#186134=CARTESIAN_POINT('Ctrl Pts',(20.8469268064436,19.3440037362855,8.07906326578301));
#186135=CARTESIAN_POINT('Ctrl Pts',(20.8581504002332,19.1313361615528,8.09215156258513));
#186136=CARTESIAN_POINT('Ctrl Pts',(20.8422458367224,18.9396507140996,8.1047899678711));
#186137=CARTESIAN_POINT('Ctrl Pts',(20.7842862355159,18.6782294747407,8.12245696833768));
#186138=CARTESIAN_POINT('Ctrl Pts',(20.7637389751389,18.604634298812,8.12746415437814));
#186139=CARTESIAN_POINT('Ctrl Pts',(20.7280420968685,18.499164863796,8.13455550064834));
#186140=CARTESIAN_POINT('Ctrl Pts',(20.7160046351787,18.4663046922486,8.13675213320625));
#186141=CARTESIAN_POINT('Ctrl Pts',(20.7004397330155,18.4268708228651,8.13935998860683));
#186142=CARTESIAN_POINT('Ctrl Pts',(20.6976859840595,18.4199999053433,8.13981332406851));
#186143=CARTESIAN_POINT('Ctrl Pts',(20.6933339324193,18.4093038452185,8.1405172296235));
#186144=CARTESIAN_POINT('Ctrl Pts',(20.6917603677301,18.4054687923196,8.14076924932889));
#186145=CARTESIAN_POINT('Ctrl Pts',(20.6888116828965,18.3983420089903,8.1412368719495));
#186146=CARTESIAN_POINT('Ctrl Pts',(20.6874395207544,18.3950491651095,8.14145264349615));
#186147=CARTESIAN_POINT('Ctrl Pts',(20.6843061062971,18.3875829672971,8.14194124462072));
#186148=CARTESIAN_POINT('Ctrl Pts',(20.6825397833067,18.3834117982039,8.14221376240389));
#186149=CARTESIAN_POINT('Ctrl Pts',(20.6772486821731,18.3710277183668,8.14302160940908));
#186150=CARTESIAN_POINT('Ctrl Pts',(20.6736852183593,18.3628313052719,8.14355464418467));
#186151=CARTESIAN_POINT('Ctrl Pts',(20.6461352954632,18.3005448034559,8.14759458454131));
#186152=CARTESIAN_POINT('Ctrl Pts',(20.6199401845378,18.2474539338933,8.15097649556824));
#186153=CARTESIAN_POINT('Ctrl Pts',(20.5145648575838,18.0546965162268,8.16327350820359));
#186154=CARTESIAN_POINT('Ctrl Pts',(20.4218098121438,17.923074186733,8.17174526433562));
#186155=CARTESIAN_POINT('Ctrl Pts',(20.2745672022251,17.7577104684876,8.18400229545833));
#186156=CARTESIAN_POINT('Ctrl Pts',(20.2321278241145,17.7139996790227,8.18742184792589));
#186157=CARTESIAN_POINT('Ctrl Pts',(20.1610674176161,17.6468622918725,8.19303391965465));
#186158=CARTESIAN_POINT('Ctrl Pts',(20.1336137003003,17.622249096882,8.19517696331534));
#186159=CARTESIAN_POINT('Ctrl Pts',(20.0970823207262,17.5911794410287,8.19800407675716));
#186160=CARTESIAN_POINT('Ctrl Pts',(20.0885758896502,17.5840592486395,8.19866069434043));
#186161=CARTESIAN_POINT('Ctrl Pts',(20.074641395364,17.5725806088952,8.199733779857));
#186162=CARTESIAN_POINT('Ctrl Pts',(20.0692470334847,17.5681814434018,8.20014858778615));
#186163=CARTESIAN_POINT('Ctrl Pts',(20.0588250506831,17.5597674360966,8.20094888717647));
#186164=CARTESIAN_POINT('Ctrl Pts',(20.0538006235375,17.5557487478618,8.20133421742802));
#186165=CARTESIAN_POINT('Ctrl Pts',(20.0422452825247,17.546592499537,8.20221932876906));
#186166=CARTESIAN_POINT('Ctrl Pts',(20.0357023140636,17.5414703868058,8.20271971859494));
#186167=CARTESIAN_POINT('Ctrl Pts',(20.0182196282748,17.5279494475271,8.20405476369801));
#186168=CARTESIAN_POINT('Ctrl Pts',(20.0072278408292,17.5196188877034,8.20489209239991));
#186169=CARTESIAN_POINT('Ctrl Pts',(19.9215454903605,17.4559896586959,8.21140444862869));
#186170=CARTESIAN_POINT('Ctrl Pts',(19.8433781122752,17.4055632812982,8.21726670638647));
#186171=CARTESIAN_POINT('Ctrl Pts',(19.6060027718017,17.2736790092296,8.23482233762077));
#186172=CARTESIAN_POINT('Ctrl Pts',(19.4395078250865,17.2070405250267,8.24689323081192));
#186173=CARTESIAN_POINT('Ctrl Pts',(19.2273536497098,17.1518889801362,8.26092083544492));
#186174=CARTESIAN_POINT('Ctrl Pts',(19.1877871272697,17.1428090616987,8.26347827670952));
#186175=CARTESIAN_POINT('Ctrl Pts',(19.1404077049916,17.133361577293,8.26645212279447));
#186176=CARTESIAN_POINT('Ctrl Pts',(19.1328258829396,17.1318928460762,8.26692532600845));
#186177=CARTESIAN_POINT('Ctrl Pts',(19.1210937720047,17.1296866701574,8.26765323915532));
#186178=CARTESIAN_POINT('Ctrl Pts',(19.1169491243575,17.128920094191,8.26790955993638));
#186179=CARTESIAN_POINT('Ctrl Pts',(19.1092982835531,17.1275286462994,8.26838114792434));
#186180=CARTESIAN_POINT('Ctrl Pts',(19.1057928291022,17.1269002480954,8.26859660908841));
#186181=CARTESIAN_POINT('Ctrl Pts',(19.0979144287942,17.1255084528918,8.26907949045741));
#186182=CARTESIAN_POINT('Ctrl Pts',(19.0935406718306,17.124749964489,8.26934662952876));
#186183=CARTESIAN_POINT('Ctrl Pts',(19.0823598875468,17.1228472199806,8.27002720940498));
#186184=CARTESIAN_POINT('Ctrl Pts',(19.0755495307269,17.1217224777507,8.27043956788783));
#186185=CARTESIAN_POINT('Ctrl Pts',(19.0360414860937,17.1153959995866,8.27281967177081));
#186186=CARTESIAN_POINT('Ctrl Pts',(19.0032289089566,17.1109282741121,8.27474860937124));
#186187=CARTESIAN_POINT('Ctrl Pts',(18.9516911818924,17.1051388753585,8.27772250434146));
#186188=CARTESIAN_POINT('Ctrl Pts',(18.9330318257708,17.1032934508825,8.27878781205925));
#186189=CARTESIAN_POINT('Ctrl Pts',(18.883191271059,17.0990319784527,8.28160866882729));
#186190=CARTESIAN_POINT('Ctrl Pts',(18.8519763573168,17.097058499626,8.2833497023143));
#186191=CARTESIAN_POINT('Ctrl Pts',(18.7822694129759,17.09420038032,8.28720197452944));
#186192=CARTESIAN_POINT('Ctrl Pts',(18.7437738949707,17.0936726361779,8.28930523651559));
#186193=CARTESIAN_POINT('Ctrl Pts',(18.5960095192937,17.0956771218647,8.2973505806258));
#186194=CARTESIAN_POINT('Ctrl Pts',(18.4870143169506,17.1056189340772,8.30323550977881));
#186195=CARTESIAN_POINT('Ctrl Pts',(18.3250240643611,17.133151057932,8.31237249763358));
#186196=CARTESIAN_POINT('Ctrl Pts',(18.2711534119266,17.1444836233796,8.31547580247535));
#186197=CARTESIAN_POINT('Ctrl Pts',(18.1845501288961,17.1662583447166,8.32061346317517));
#186198=CARTESIAN_POINT('Ctrl Pts',(18.1515215748684,17.17542089666,8.32260855877994));
#186199=CARTESIAN_POINT('Ctrl Pts',(18.1083928119074,17.1885209787743,8.32526690027165));
#186200=CARTESIAN_POINT('Ctrl Pts',(18.098078683079,17.1917402798983,8.32590666984632));
#186201=CARTESIAN_POINT('Ctrl Pts',(18.0812216954589,17.1971437346074,8.32695908639587));
#186202=CARTESIAN_POINT('Ctrl Pts',(18.0746639872074,17.1992811843987,8.32737019375435));
#186203=CARTESIAN_POINT('Ctrl Pts',(18.061987450785,17.2034816740516,8.32816823249805));
#186204=CARTESIAN_POINT('Ctrl Pts',(18.0558673791814,17.2055407402618,8.32855502888172));
#186205=CARTESIAN_POINT('Ctrl Pts',(18.0417538772983,17.2103611457819,8.32945056398271));
#186206=CARTESIAN_POINT('Ctrl Pts',(18.0337674220228,17.2131424342812,8.32995995955124));
#186207=CARTESIAN_POINT('Ctrl Pts',(18.012324168172,17.2207544340201,8.33133486860982));
#186208=CARTESIAN_POINT('Ctrl Pts',(17.9988994684668,17.2256736762072,8.3322033141505));
#186209=CARTESIAN_POINT('Ctrl Pts',(17.8756709986461,17.2722497730966,8.34024723633983));
#186210=CARTESIAN_POINT('Ctrl Pts',(17.769479780301,17.3228331793544,8.34772770571448));
#186211=CARTESIAN_POINT('Ctrl Pts',(17.5265483705793,17.4644118186841,8.3660979523529));
#186212=CARTESIAN_POINT('Ctrl Pts',(17.3951035362788,17.5630114445614,8.37712898107205));
#186213=CARTESIAN_POINT('Ctrl Pts',(17.2538230711235,17.6971541617917,8.38949101684688));
#186214=CARTESIAN_POINT('Ctrl Pts',(17.2317792069455,17.7190261773293,8.39143495321358));
#186215=CARTESIAN_POINT('Ctrl Pts',(17.2052685506064,17.7465137095053,8.39378276704108));
#186216=CARTESIAN_POINT('Ctrl Pts',(17.2003398386427,17.7516760290386,8.39421969567358));
#186217=CARTESIAN_POINT('Ctrl Pts',(17.192629870127,17.7598336321366,8.3949037271252));
#186218=CARTESIAN_POINT('Ctrl Pts',(17.1898310723782,17.762812157176,8.39515215187031));
#186219=CARTESIAN_POINT('Ctrl Pts',(17.184600121321,17.7684114241679,8.39561663993207));
#186220=CARTESIAN_POINT('Ctrl Pts',(17.182166009356,17.771030191683,8.39583285027263));
#186221=CARTESIAN_POINT('Ctrl Pts',(17.1766043152108,17.7770442858546,8.39632704935111));
#186222=CARTESIAN_POINT('Ctrl Pts',(17.1734812015795,17.7804436782034,8.39660469720257));
#186223=CARTESIAN_POINT('Ctrl Pts',(17.1638449847441,17.7910014473595,8.39746188811729));
#186224=CARTESIAN_POINT('Ctrl Pts',(17.1573697247597,17.7981944066286,8.3980386390588));
#186225=CARTESIAN_POINT('Ctrl Pts',(17.0888253216945,17.8753942370954,8.40415509099116));
#186226=CARTESIAN_POINT('Ctrl Pts',(17.0314046947335,17.9494072864013,8.40937985767366));
#186227=CARTESIAN_POINT('Ctrl Pts',(16.9052198389649,18.136437404125,8.42175707314412));
#186228=CARTESIAN_POINT('Ctrl Pts',(16.8417777130446,18.2525550238779,8.42880642862429));
#186229=CARTESIAN_POINT('Ctrl Pts',(16.7672717976745,18.4256038862872,8.43927195419713));
#186230=CARTESIAN_POINT('Ctrl Pts',(16.7470574656025,18.478247955487,8.44244770343866));
#186231=CARTESIAN_POINT('Ctrl Pts',(16.7177768299157,18.5646645950144,8.44769447419419));
#186232=CARTESIAN_POINT('Ctrl Pts',(16.7074032722856,18.5979658864742,8.44972401166756));
#186233=CARTESIAN_POINT('Ctrl Pts',(16.6948809049371,18.6419652442051,8.45242171561416));
#186234=CARTESIAN_POINT('Ctrl Pts',(16.6919850793439,18.6524462476225,8.45306550904215));
#186235=CARTESIAN_POINT('Ctrl Pts',(16.687380676545,18.6696257059902,8.45412285921641));
#186236=CARTESIAN_POINT('Ctrl Pts',(16.685623914715,18.6763111251912,8.45453484790281));
#186237=CARTESIAN_POINT('Ctrl Pts',(16.6822909630623,18.689252315848,8.45533339897452));
#186238=CARTESIAN_POINT('Ctrl Pts',(16.6807105628131,18.6955069313001,8.45571982000635));
#186239=CARTESIAN_POINT('Ctrl Pts',(16.6771333681718,18.7099415620988,8.45661274807098));
#186240=CARTESIAN_POINT('Ctrl Pts',(16.675156749043,18.7181264217778,8.45711989992978));
#186241=CARTESIAN_POINT('Ctrl Pts',(16.6699846633705,18.7401173122278,8.45848483941948));
#186242=CARTESIAN_POINT('Ctrl Pts',(16.6668789475786,18.7539438165892,8.45934549332977));
#186243=CARTESIAN_POINT('Ctrl Pts',(16.6325818105057,18.9141381136881,8.46934707087851));
#186244=CARTESIAN_POINT('Ctrl Pts',(16.6168624934387,19.0633573065227,8.47899859422792));
#186245=CARTESIAN_POINT('Ctrl Pts',(16.617139476207,19.3627302310582,8.4987281552706));
#186246=CARTESIAN_POINT('Ctrl Pts',(16.6331712122024,19.5120733058891,8.50874331273543));
#186247=CARTESIAN_POINT('Ctrl Pts',(16.6681544975782,19.6738371178254,8.5190680570008));
#186248=CARTESIAN_POINT('Ctrl Pts',(16.671646380716,19.6891562714579,8.52004014896673));
#186249=CARTESIAN_POINT('Ctrl Pts',(16.6766589553007,19.7100695241367,8.52135811742987));
#186250=CARTESIAN_POINT('Ctrl Pts',(16.6780324478114,19.7156979198373,8.52171191625856));
#186251=CARTESIAN_POINT('Ctrl Pts',(16.6802514660234,19.7246317736394,8.52227197438837));
#186252=CARTESIAN_POINT('Ctrl Pts',(16.6810818949222,19.7279408998413,8.52247908939753));
#186253=CARTESIAN_POINT('Ctrl Pts',(16.6828132675962,19.7347701706098,8.52290581951831));
#186254=CARTESIAN_POINT('Ctrl Pts',(16.6837152750071,19.7382900050455,8.52312536596812));
#186255=CARTESIAN_POINT('Ctrl Pts',(16.6858857791743,19.7466700183093,8.52364716007648));
#186256=CARTESIAN_POINT('Ctrl Pts',(16.687162529565,19.7515280759319,8.52394893195275));
#186257=CARTESIAN_POINT('Ctrl Pts',(16.6915249191881,19.7678899359836,8.52496299930673));
#186258=CARTESIAN_POINT('Ctrl Pts',(16.6946904096531,19.7793724711379,8.52567082640978));
#186259=CARTESIAN_POINT('Ctrl Pts',(16.7120038266166,19.8401679778402,8.5294010897818));
#186260=CARTESIAN_POINT('Ctrl Pts',(16.7278379789767,19.8889605106395,8.53233405544009));
#186261=CARTESIAN_POINT('Ctrl Pts',(16.7454193934539,19.9371103024118,8.53521106676425));
#186262=CARTESIAN_POINT('Origin',(18.734,19.211,0.));
#186263=CARTESIAN_POINT('',(16.7437494103711,19.9377357416701,9.55561790998273));
#186264=CARTESIAN_POINT('',(16.7454193811439,19.9371102686989,9.33206801830578));
#186265=CARTESIAN_POINT('',(16.7454193623258,19.9371102171621,0.));
#186266=CARTESIAN_POINT('',(16.616352496962,19.2128935159974,9.51094372097751));
#186267=CARTESIAN_POINT('Ctrl Pts',(16.616352496962,19.2128935159974,9.51094372097751));
#186268=CARTESIAN_POINT('Ctrl Pts',(16.6150297892913,19.3558822368192,9.51955279572482));
#186269=CARTESIAN_POINT('Ctrl Pts',(16.6379357136472,19.6027931032506,9.5344441920599));
#186270=CARTESIAN_POINT('Ctrl Pts',(16.7071052565872,19.8401886875416,9.54933558839497));
#186271=CARTESIAN_POINT('Ctrl Pts',(16.7437494103711,19.9377357416701,9.55561790998273));
#186272=CARTESIAN_POINT('Ctrl Pts',(16.6170008641642,19.2129128174038,9.51057059174555));
#186273=CARTESIAN_POINT('Ctrl Pts',(16.6168631868029,19.0605392273433,9.50228575561247));
#186274=CARTESIAN_POINT('Ctrl Pts',(16.6331756165184,18.9086044877191,9.49407331105422));
#186275=CARTESIAN_POINT('Ctrl Pts',(16.6710117387555,18.7351851106024,9.48389303380534));
#186276=CARTESIAN_POINT('Ctrl Pts',(16.6768043973513,18.7107335185976,9.48243957060468));
#186277=CARTESIAN_POINT('Ctrl Pts',(16.6862549747941,18.6737862621852,9.48021287530327));
#186278=CARTESIAN_POINT('Ctrl Pts',(16.6895953042397,18.6612112067376,9.47944961775237));
#186279=CARTESIAN_POINT('Ctrl Pts',(16.6960056019571,18.637945435653,9.47802702852224));
#186280=CARTESIAN_POINT('Ctrl Pts',(16.6990443286782,18.6272465342369,9.47736871703937));
#186281=CARTESIAN_POINT('Ctrl Pts',(16.7041234695228,18.6098853584401,9.47629355189756));
#186282=CARTESIAN_POINT('Ctrl Pts',(16.7061127423382,18.6032082513643,9.47587837053529));
#186283=CARTESIAN_POINT('Ctrl Pts',(16.7100017484915,18.5903862345436,9.47507782781616));
#186284=CARTESIAN_POINT('Ctrl Pts',(16.711896599253,18.5842399157133,9.47469263024993));
#186285=CARTESIAN_POINT('Ctrl Pts',(16.7162994341446,18.5701862658294,9.47380849840893));
#186286=CARTESIAN_POINT('Ctrl Pts',(16.7188259343314,18.5622848873713,9.4733089599268));
#186287=CARTESIAN_POINT('Ctrl Pts',(16.7256616973275,18.5413320444977,9.47197766285819));
#186288=CARTESIAN_POINT('Ctrl Pts',(16.7300516812434,18.5283075140467,9.47114325456751));
#186289=CARTESIAN_POINT('Ctrl Pts',(16.7645088008198,18.4292744148387,9.46474530371271));
#186290=CARTESIAN_POINT('Ctrl Pts',(16.7999694901022,18.3452560210027,9.45900206102836));
#186291=CARTESIAN_POINT('Ctrl Pts',(16.8622522444355,18.2207657410432,9.45001095382446));
#186292=CARTESIAN_POINT('Ctrl Pts',(16.8852374914198,18.1784883159323,9.44686823633246));
#186293=CARTESIAN_POINT('Ctrl Pts',(16.9358507399165,18.0925111726021,9.44030887825123));
#186294=CARTESIAN_POINT('Ctrl Pts',(16.9636801260305,18.0489649597478,9.4368912216606));
#186295=CARTESIAN_POINT('Ctrl Pts',(17.0410581348755,17.9371282998117,9.42790784999361));
#186296=CARTESIAN_POINT('Ctrl Pts',(17.0931467175513,17.8707001764926,9.42235623719979));
#186297=CARTESIAN_POINT('Ctrl Pts',(17.1736468430556,17.779789947113,9.41460812106404));
#186298=CARTESIAN_POINT('Ctrl Pts',(17.198958106632,17.7526752887502,9.41227648247279));
#186299=CARTESIAN_POINT('Ctrl Pts',(17.2302643853823,17.7208573297973,9.40952976152539));
#186300=CARTESIAN_POINT('Ctrl Pts',(17.2355872031759,17.7155050750742,9.4090673497681));
#186301=CARTESIAN_POINT('Ctrl Pts',(17.2439050643718,17.7072302065798,9.4083520236153));
#186302=CARTESIAN_POINT('Ctrl Pts',(17.2468802759877,17.7042878722394,9.40809758960079));
#186303=CARTESIAN_POINT('Ctrl Pts',(17.2524054123862,17.6988560991563,9.40762776709647));
#186304=CARTESIAN_POINT('Ctrl Pts',(17.2549528770421,17.6963642988243,9.40741219569709));
#186305=CARTESIAN_POINT('Ctrl Pts',(17.260715228745,17.6907562602201,9.40692692315031));
#186306=CARTESIAN_POINT('Ctrl Pts',(17.2639337075602,17.6876437901032,9.40665751609366));
#186307=CARTESIAN_POINT('Ctrl Pts',(17.2734297528344,17.6785186421983,9.40586734374596));
#186308=CARTESIAN_POINT('Ctrl Pts',(17.2797345928115,17.6725343064488,9.40534872659042));
#186309=CARTESIAN_POINT('Ctrl Pts',(17.3245664470674,17.6305033307233,9.40170171030165));
#186310=CARTESIAN_POINT('Ctrl Pts',(17.3643957203279,17.5958660214916,9.39867246161717));
#186311=CARTESIAN_POINT('Ctrl Pts',(17.4205669785028,17.5505909739008,9.39461311580937));
#186312=CARTESIAN_POINT('Ctrl Pts',(17.4358193874765,17.5386389250701,9.39353122639919));
#186313=CARTESIAN_POINT('Ctrl Pts',(17.60170288466,17.4122869186503,9.38195672191991));
#186314=CARTESIAN_POINT('Ctrl Pts',(17.766848813507,17.3183592594585,9.37203060454308));
#186315=CARTESIAN_POINT('Ctrl Pts',(17.9921022215736,17.2275277199031,9.35827028911597));
#186316=CARTESIAN_POINT('Ctrl Pts',(18.0426651317156,17.2093431889747,9.3551752436795));
#186317=CARTESIAN_POINT('Ctrl Pts',(18.105898312267,17.1892837183624,9.35127299965955));
#186318=CARTESIAN_POINT('Ctrl Pts',(18.1179684008066,17.1855732518881,9.35052677202271));
#186319=CARTESIAN_POINT('Ctrl Pts',(18.1370676250858,17.1798884735445,9.34934354915956));
#186320=CARTESIAN_POINT('Ctrl Pts',(18.1440751386236,17.1778421239354,9.34890891306893));
#186321=CARTESIAN_POINT('Ctrl Pts',(18.15721380775,17.1740789839324,9.34809298391168));
#186322=CARTESIAN_POINT('Ctrl Pts',(18.1633424107606,17.1723535245805,9.34771197864494));
#186323=CARTESIAN_POINT('Ctrl Pts',(18.1770509902638,17.168560642189,9.346858781466));
#186324=CARTESIAN_POINT('Ctrl Pts',(18.1846348513574,17.1665077254628,9.34638612393971));
#186325=CARTESIAN_POINT('Ctrl Pts',(18.2038347157889,17.1614249509809,9.34518778721889));
#186326=CARTESIAN_POINT('Ctrl Pts',(18.2154652744089,17.1584516231797,9.34446029070854));
#186327=CARTESIAN_POINT('Ctrl Pts',(18.2811550344823,17.1422521293461,9.34034192892597));
#186328=CARTESIAN_POINT('Ctrl Pts',(18.3356897791891,17.1310638529534,9.33688613978704));
#186329=CARTESIAN_POINT('Ctrl Pts',(18.4151676168696,17.1179985950006,9.33179366450893));
#186330=CARTESIAN_POINT('Ctrl Pts',(18.4398056387823,17.1143935573068,9.33020744464369));
#186331=CARTESIAN_POINT('Ctrl Pts',(18.6245700875342,17.0906796617505,9.31825943560445));
#186332=CARTESIAN_POINT('Ctrl Pts',(18.7864580297341,17.0885079834089,9.30743879571178));
#186333=CARTESIAN_POINT('Ctrl Pts',(18.9957245827716,17.1096698884429,9.29371319855008));
#186334=CARTESIAN_POINT('Ctrl Pts',(19.0442732601583,17.1162878162427,9.29055236422752));
#186335=CARTESIAN_POINT('Ctrl Pts',(19.1184282446578,17.1290313877083,9.28580100344138));
#186336=CARTESIAN_POINT('Ctrl Pts',(19.1442213675224,17.1339595684642,9.28416283081811));
#186337=CARTESIAN_POINT('Ctrl Pts',(19.1765321006913,17.1407584607714,9.28213458330725));
#186338=CARTESIAN_POINT('Ctrl Pts',(19.1831401500072,17.1421820236199,9.28172103889861));
#186339=CARTESIAN_POINT('Ctrl Pts',(19.1936508829726,17.1444990702068,9.28106539596722));
#186340=CARTESIAN_POINT('Ctrl Pts',(19.1975579811754,17.1453720020882,9.28082214902407));
#186341=CARTESIAN_POINT('Ctrl Pts',(19.2049669237299,17.1470494031167,9.28036181190379));
#186342=CARTESIAN_POINT('Ctrl Pts',(19.208469151896,17.1478516937275,9.28014460674308));
#186343=CARTESIAN_POINT('Ctrl Pts',(19.216530265755,17.1497199458845,9.27964555528487));
#186344=CARTESIAN_POINT('Ctrl Pts',(19.2210876681024,17.1507921164578,9.2793640687497));
#186345=CARTESIAN_POINT('Ctrl Pts',(19.2333014469556,17.1537083132556,9.27861135622915));
#186346=CARTESIAN_POINT('Ctrl Pts',(19.2409512372471,17.1555799780351,9.27814167452741));
#186347=CARTESIAN_POINT('Ctrl Pts',(19.2983968703626,17.1699753505868,9.27462666534343));
#186348=CARTESIAN_POINT('Ctrl Pts',(19.3477370871842,17.1842653962878,9.27167563681548));
#186349=CARTESIAN_POINT('Ctrl Pts',(19.4099920486199,17.2047783855212,9.26798314539287));
#186350=CARTESIAN_POINT('Ctrl Pts',(19.4234265164141,17.2093552992916,9.26718819872463));
#186351=CARTESIAN_POINT('Ctrl Pts',(19.5717313164452,17.261550698438,9.25842355480264));
#186352=CARTESIAN_POINT('Ctrl Pts',(19.7014932310011,17.3225861032539,9.25082984792975));
#186353=CARTESIAN_POINT('Ctrl Pts',(19.9038144242271,17.4441192728222,9.23783195354945));
#186354=CARTESIAN_POINT('Ctrl Pts',(19.9802661958951,17.4971881769649,9.23261193212216));
#186355=CARTESIAN_POINT('Ctrl Pts',(20.0694828619276,17.5682523680661,9.22596822607224));
#186356=CARTESIAN_POINT('Ctrl Pts',(20.0857899748102,17.5816448903583,9.2247298216473));
#186357=CARTESIAN_POINT('Ctrl Pts',(20.1087325361757,17.6010684036486,9.22295148212606));
#186358=CARTESIAN_POINT('Ctrl Pts',(20.1155344106663,17.606901511959,9.22241963578056));
#186359=CARTESIAN_POINT('Ctrl Pts',(20.1272193417023,17.6170516495772,9.22149786041159));
#186360=CARTESIAN_POINT('Ctrl Pts',(20.1321199066549,17.6213484019889,9.22110877554216));
#186361=CARTESIAN_POINT('Ctrl Pts',(20.1414751013927,17.629627639607,9.22036116106304));
#186362=CARTESIAN_POINT('Ctrl Pts',(20.1459328709478,17.633606494861,9.22000278569393));
#186363=CARTESIAN_POINT('Ctrl Pts',(20.1575027846565,17.6440217513706,9.2190670187211));
#186364=CARTESIAN_POINT('Ctrl Pts',(20.1645880749135,17.650487659523,9.21848838232287));
#186365=CARTESIAN_POINT('Ctrl Pts',(20.1887107133792,17.6728039003838,9.21649893120954));
#186366=CARTESIAN_POINT('Ctrl Pts',(20.205530062419,17.6888864339084,9.21507820400915));
#186367=CARTESIAN_POINT('Ctrl Pts',(20.3440123295447,17.8257429593144,9.20309096646443));
#186368=CARTESIAN_POINT('Ctrl Pts',(20.4508344127262,17.9605862841972,9.19185696588243));
#186369=CARTESIAN_POINT('Ctrl Pts',(20.5871011322324,18.1834859995083,9.17459316183655));
#186370=CARTESIAN_POINT('Ctrl Pts',(20.6290565811356,18.2630910549778,9.16866181252265));
#186371=CARTESIAN_POINT('Ctrl Pts',(20.6815899466365,18.3802967761655,9.16045645100884));
#186372=CARTESIAN_POINT('Ctrl Pts',(20.6963915809533,18.4158936163153,9.15803093408932));
#186373=CARTESIAN_POINT('Ctrl Pts',(20.712943609435,18.4589832862587,9.15519024378226));
#186374=CARTESIAN_POINT('Ctrl Pts',(20.7156349591384,18.4661041416202,9.15472387695126));
#186375=CARTESIAN_POINT('Ctrl Pts',(20.7197484392224,18.4771677977887,9.15400421690796));
#186376=CARTESIAN_POINT('Ctrl Pts',(20.7211973375232,18.4811004813538,9.15374936914788));
#186377=CARTESIAN_POINT('Ctrl Pts',(20.7238563932898,18.4883844527164,9.15327916280796));
#186378=CARTESIAN_POINT('Ctrl Pts',(20.7250697590424,18.4917344648692,9.15306361888813));
#186379=CARTESIAN_POINT('Ctrl Pts',(20.7277858647258,18.4992929715216,9.1525788857334));
#186380=CARTESIAN_POINT('Ctrl Pts',(20.7292837361619,18.5035031577345,9.15230998768544));
#186381=CARTESIAN_POINT('Ctrl Pts',(20.7336427672952,18.5158793828259,9.1515226901763));
#186382=CARTESIAN_POINT('Ctrl Pts',(20.7364672462755,18.5240583703047,9.15100641550432));
#186383=CARTESIAN_POINT('Ctrl Pts',(20.7558471715588,18.5813131695926,9.14741889934705));
#186384=CARTESIAN_POINT('Ctrl Pts',(20.7706483470256,18.6309690169995,9.14444316253679));
#186385=CARTESIAN_POINT('Ctrl Pts',(20.7889950504447,18.7019356560429,9.14031552488931));
#186386=CARTESIAN_POINT('Ctrl Pts',(20.7940587001143,18.7228306040054,9.13911531609063));
#186387=CARTESIAN_POINT('Ctrl Pts',(20.8292197080863,18.8782254933424,9.13027766202423));
#186388=CARTESIAN_POINT('Ctrl Pts',(20.8464369297966,19.0153028105548,9.12294747445923));
#186389=CARTESIAN_POINT('Ctrl Pts',(20.8526907767981,19.2438180023166,9.11034417241446));
#186390=CARTESIAN_POINT('Ctrl Pts',(20.8493359483967,19.334607113795,9.10524185800939));
#186391=CARTESIAN_POINT('Ctrl Pts',(20.8380618606554,19.4456202746019,9.09874056226291));
#186392=CARTESIAN_POINT('Ctrl Pts',(20.8356512762426,19.4663132470701,9.09751770070753));
#186393=CARTESIAN_POINT('Ctrl Pts',(20.8317736957737,19.4958051783106,9.09575783048884));
#186394=CARTESIAN_POINT('Ctrl Pts',(20.8305558231179,19.504636075985,9.09522867922539));
#186395=CARTESIAN_POINT('Ctrl Pts',(20.8283522331054,19.5199014318079,9.09431008629121));
#186396=CARTESIAN_POINT('Ctrl Pts',(20.827392540083,19.5263395670572,9.09392147289336));
#186397=CARTESIAN_POINT('Ctrl Pts',(20.8254934472971,19.538688851528,9.09317371420938));
#186398=CARTESIAN_POINT('Ctrl Pts',(20.8245586400775,19.5446006516122,9.09281471812043));
#186399=CARTESIAN_POINT('Ctrl Pts',(20.8220516521553,19.5600306071277,9.09187499391617));
#186400=CARTESIAN_POINT('Ctrl Pts',(20.8204394712529,19.5695420404342,9.09129300025844));
#186401=CARTESIAN_POINT('Ctrl Pts',(20.8146594185818,19.6022829672878,9.0892800458128));
#186402=CARTESIAN_POINT('Ctrl Pts',(20.8101682690658,19.6254529218304,9.08783885528337));
#186403=CARTESIAN_POINT('Ctrl Pts',(20.7711451420421,19.8101853620767,9.07621038718791));
#186404=CARTESIAN_POINT('Ctrl Pts',(20.7182011930178,19.9672468774428,9.0654086352931));
#186405=CARTESIAN_POINT('Ctrl Pts',(20.5930554604647,20.2317049056693,9.04607413444419));
#186406=CARTESIAN_POINT('Ctrl Pts',(20.5282578836148,20.3417391809126,9.0376464110774));
#186407=CARTESIAN_POINT('Ctrl Pts',(20.4469596193446,20.4550265677872,9.02899833398777));
#186408=CARTESIAN_POINT('Ctrl Pts',(20.4398862408848,20.4647084618394,9.02825962761895));
#186409=CARTESIAN_POINT('Ctrl Pts',(20.4297252408377,20.4783714033376,9.02721834065978));
#186410=CARTESIAN_POINT('Ctrl Pts',(20.426705231929,20.4824021257711,9.02691129487356));
#186411=CARTESIAN_POINT('Ctrl Pts',(20.4214803329305,20.4893240378003,9.02638431608451));
#186412=CARTESIAN_POINT('Ctrl Pts',(20.4192823357679,20.4922203827491,9.02616390552331));
#186413=CARTESIAN_POINT('Ctrl Pts',(20.415009655659,20.4978205593769,9.0257379367387));
#186414=CARTESIAN_POINT('Ctrl Pts',(20.412935905607,20.5005250442304,9.02553231331246));
#186415=CARTESIAN_POINT('Ctrl Pts',(20.4073307962305,20.5077985163791,9.02497951222334));
#186416=CARTESIAN_POINT('Ctrl Pts',(20.4037872285638,20.5123581208878,9.02463319020381));
#186417=CARTESIAN_POINT('Ctrl Pts',(20.3906101418841,20.5291709985758,9.02335675283312));
#186418=CARTESIAN_POINT('Ctrl Pts',(20.3808597747519,20.541332611756,9.02243457556222));
#186419=CARTESIAN_POINT('Ctrl Pts',(20.2842999522995,20.6590827224316,9.01350484426809));
#186420=CARTESIAN_POINT('Ctrl Pts',(20.187578319304,20.756151758549,9.0061213883061));
#186421=CARTESIAN_POINT('Ctrl Pts',(19.9630191764834,20.9416295759864,8.99030479204379));
#186422=CARTESIAN_POINT('Ctrl Pts',(19.8334804035951,21.0266823094003,8.98188541975609));
#186423=CARTESIAN_POINT('Ctrl Pts',(19.6768994407564,21.106542681726,8.97164903787487));
#186424=CARTESIAN_POINT('Ctrl Pts',(19.6578075221962,21.1159202153943,8.97040086726002));
#186425=CARTESIAN_POINT('Ctrl Pts',(19.6304507513228,21.1288492789825,8.96861093279639));
#186426=CARTESIAN_POINT('Ctrl Pts',(19.6222991730791,21.1326384628103,8.968077404776));
#186427=CARTESIAN_POINT('Ctrl Pts',(19.6081915297166,21.139087320333,8.9671536403025));
#186428=CARTESIAN_POINT('Ctrl Pts',(19.6022468067036,21.1417716143131,8.9667642579435));
#186429=CARTESIAN_POINT('Ctrl Pts',(19.5908383018242,21.1468596940281,8.966016719406));
#186430=CARTESIAN_POINT('Ctrl Pts',(19.5853765647875,21.1492679314873,8.96565872058304));
#186431=CARTESIAN_POINT('Ctrl Pts',(19.57114234161,21.1554724394587,8.9647253646448));
#186432=CARTESIAN_POINT('Ctrl Pts',(19.5623542716346,21.1592324204027,8.96414877533224));
#186433=CARTESIAN_POINT('Ctrl Pts',(19.5322725792559,21.1718625611146,8.96217375435025));
#186434=CARTESIAN_POINT('Ctrl Pts',(19.5108601721294,21.1804439066081,8.96076560306096));
#186435=CARTESIAN_POINT('Ctrl Pts',(19.3263064582098,21.2509286086192,8.94860481058065));
#186436=CARTESIAN_POINT('Ctrl Pts',(19.1562580037787,21.2927806783011,8.93715751326993));
#186437=CARTESIAN_POINT('Ctrl Pts',(18.8959421557957,21.3236185655257,8.91983712157592));
#186438=CARTESIAN_POINT('Ctrl Pts',(18.8082760677541,21.3285144546901,8.91405462361345));
#186439=CARTESIAN_POINT('Ctrl Pts',(18.6825554902011,21.3277159560012,8.90602654579139));
#186440=CARTESIAN_POINT('Ctrl Pts',(18.6445671356337,21.326451524889,8.90363598349833));
#186441=CARTESIAN_POINT('Ctrl Pts',(18.5990627653466,21.323708788843,8.90083069806408));
#186442=CARTESIAN_POINT('Ctrl Pts',(18.5914970692073,21.3232119691119,8.90036622133922));
#186443=CARTESIAN_POINT('Ctrl Pts',(18.579760167528,21.3223778874392,8.8996488445639));
#186444=CARTESIAN_POINT('Ctrl Pts',(18.5755871066085,21.3220688916743,8.89939440537963));
#186445=CARTESIAN_POINT('Ctrl Pts',(18.5678619271626,21.3214738424368,8.89892457809114));
#186446=CARTESIAN_POINT('Ctrl Pts',(18.5643096452303,21.3211911957582,8.89870900704697));
#186447=CARTESIAN_POINT('Ctrl Pts',(18.5562959081252,21.3205331948837,8.89822374129377));
#186448=CARTESIAN_POINT('Ctrl Pts',(18.5518349327937,21.3201526577566,8.897954340639));
#186449=CARTESIAN_POINT('Ctrl Pts',(18.5387170287883,21.3189917246913,8.89716420447811));
#186450=CARTESIAN_POINT('Ctrl Pts',(18.530063539453,21.3181721515184,8.89664561681286));
#186451=CARTESIAN_POINT('Ctrl Pts',(18.468943507397,21.3120034216941,8.89299994260129));
#186452=CARTESIAN_POINT('Ctrl Pts',(18.4166832720523,21.3047481713275,8.88997192145887));
#186453=CARTESIAN_POINT('Ctrl Pts',(18.3492011147206,21.2927944152816,8.88611580775541));
#186454=CARTESIAN_POINT('Ctrl Pts',(18.3336889852804,21.2898673066634,8.8852331521866));
#186455=CARTESIAN_POINT('Ctrl Pts',(18.2683586240147,21.2767812228372,8.88152638802928));
#186456=CARTESIAN_POINT('Ctrl Pts',(18.2188806346554,21.2650025168272,8.87874487300235));
#186457=CARTESIAN_POINT('Ctrl Pts',(18.0644204639103,21.2222987187503,8.87001963641199));
#186458=CARTESIAN_POINT('Ctrl Pts',(17.9613874627891,21.1850132425348,8.86412865608804));
#186459=CARTESIAN_POINT('Ctrl Pts',(17.8114225751872,21.1171964404653,8.85497760027843));
#186460=CARTESIAN_POINT('Ctrl Pts',(17.7620546699484,21.0925035483122,8.85186623188849));
#186461=CARTESIAN_POINT('Ctrl Pts',(17.6836215478701,21.0493615891663,8.84671641334545));
#186462=CARTESIAN_POINT('Ctrl Pts',(17.6539415372318,21.032082575034,8.84471746757898));
#186463=CARTESIAN_POINT('Ctrl Pts',(17.6154867519729,21.008424275622,8.84205472349388));
#186464=CARTESIAN_POINT('Ctrl Pts',(17.6063211138068,21.0026880966497,8.84141450086276));
#186465=CARTESIAN_POINT('Ctrl Pts',(17.5913800242238,20.9931773724797,8.84036152887099));
#186466=CARTESIAN_POINT('Ctrl Pts',(17.5855782992451,20.9894443178026,8.83995032231926));
#186467=CARTESIAN_POINT('Ctrl Pts',(17.5743824825011,20.9821628664757,8.83915222667252));
#186468=CARTESIAN_POINT('Ctrl Pts',(17.5689861667969,20.978618016848,8.83876547329724));
#186469=CARTESIAN_POINT('Ctrl Pts',(17.5565627272509,20.9703754338939,8.83787023536037));
#186470=CARTESIAN_POINT('Ctrl Pts',(17.5495473896912,20.9656602119338,8.83736109531864));
#186471=CARTESIAN_POINT('Ctrl Pts',(17.5307542220067,20.9528646917018,8.83598732310633));
#186472=CARTESIAN_POINT('Ctrl Pts',(17.5190297750097,20.9447071099665,8.835119766423));
#186473=CARTESIAN_POINT('Ctrl Pts',(17.3924219245189,20.8547014690873,8.82563478892659));
#186474=CARTESIAN_POINT('Ctrl Pts',(17.2859326259487,20.7617010618435,8.81656767221894));
#186475=CARTESIAN_POINT('Ctrl Pts',(17.1234054373051,20.5883208351413,8.80093329491484));
#186476=CARTESIAN_POINT('Ctrl Pts',(17.0622207724101,20.5133754994165,8.79450512456632));
#186477=CARTESIAN_POINT('Ctrl Pts',(16.9686661036172,20.381273955029,8.78394198541052));
#186478=CARTESIAN_POINT('Ctrl Pts',(16.9334397172737,20.3263157397975,8.77974785945581));
#186479=CARTESIAN_POINT('Ctrl Pts',(16.8942250423268,20.2584207346613,8.7748764161203));
#186480=CARTESIAN_POINT('Ctrl Pts',(16.887751058384,20.246966677005,8.7740648272924));
#186481=CARTESIAN_POINT('Ctrl Pts',(16.8788540528302,20.2308773697379,8.77293982866617));
#186482=CARTESIAN_POINT('Ctrl Pts',(16.8763409391769,20.2262926423885,8.772620943944));
#186483=CARTESIAN_POINT('Ctrl Pts',(16.8720920954119,20.2184727949759,8.77207997594959));
#186484=CARTESIAN_POINT('Ctrl Pts',(16.8703477577309,20.2152424002171,8.77185734856318));
#186485=CARTESIAN_POINT('Ctrl Pts',(16.8670223269156,20.2090454239041,8.77143191907515));
#186486=CARTESIAN_POINT('Ctrl Pts',(16.8654398911147,20.206079604765,8.77122902887216));
#186487=CARTESIAN_POINT('Ctrl Pts',(16.8612708338858,20.1982208977377,8.77069327944462));
#186488=CARTESIAN_POINT('Ctrl Pts',(16.8586963034075,20.1933215754845,8.77036118282769));
#186489=CARTESIAN_POINT('Ctrl Pts',(16.8496512051845,20.175943625713,8.76918975715014));
#186490=CARTESIAN_POINT('Ctrl Pts',(16.8432855755135,20.163410400007,8.76835677297196));
#186491=CARTESIAN_POINT('Ctrl Pts',(16.8025847883873,20.0812584720126,8.76296776030849));
#186492=CARTESIAN_POINT('Ctrl Pts',(16.7720027251434,20.0099134727692,8.75861676559915));
#186493=CARTESIAN_POINT('Ctrl Pts',(16.7454192421517,19.937109888044,8.75434672885778));
#186494=CARTESIAN_POINT('',(16.6170000979998,19.2103558486173,9.29097292758594));
#186495=CARTESIAN_POINT('Ctrl Pts',(16.7454193934539,19.9371103024118,8.53521106676425));
#186496=CARTESIAN_POINT('Ctrl Pts',(16.7707333790309,20.0064370983899,8.5393534310353));
#186497=CARTESIAN_POINT('Ctrl Pts',(16.7996695295206,20.074431401749,8.54338075368839));
#186498=CARTESIAN_POINT('Ctrl Pts',(16.9057915083873,20.291498613237,8.55651367139851));
#186499=CARTESIAN_POINT('Ctrl Pts',(16.997098875721,20.432880142472,8.56556714308397));
#186500=CARTESIAN_POINT('Ctrl Pts',(17.1191104677879,20.58007705896,8.57667156062985));
#186501=CARTESIAN_POINT('Ctrl Pts',(17.1343922602669,20.5979012974354,8.57804656005877));
#186502=CARTESIAN_POINT('Ctrl Pts',(17.1563534133947,20.6226702588014,8.58000255688896));
#186503=CARTESIAN_POINT('Ctrl Pts',(17.1627889130972,20.6298295836901,8.58057339999643));
#186504=CARTESIAN_POINT('Ctrl Pts',(17.1733019002434,20.6413657643934,8.58150227841002));
#186505=CARTESIAN_POINT('Ctrl Pts',(17.1773495484935,20.6457697199295,8.58185904757045));
#186506=CARTESIAN_POINT('Ctrl Pts',(17.1858429072387,20.6549324867784,8.58260591348199));
#186507=CARTESIAN_POINT('Ctrl Pts',(17.1902920153215,20.6596880502063,8.58299615365754));
#186508=CARTESIAN_POINT('Ctrl Pts',(17.2008948676105,20.6709169239469,8.58392385193664));
#186509=CARTESIAN_POINT('Ctrl Pts',(17.2070677383426,20.6773719297212,8.5844621338399));
#186510=CARTESIAN_POINT('Ctrl Pts',(17.2278430917356,20.6988234074668,8.58626788715645));
#186511=CARTESIAN_POINT('Ctrl Pts',(17.2426267489851,20.7136419736238,8.58754326790624));
#186512=CARTESIAN_POINT('Ctrl Pts',(17.3232616674467,20.7921050453753,8.59445099681882));
#186513=CARTESIAN_POINT('Ctrl Pts',(17.3929624739339,20.8516371852736,8.60025765400415));
#186514=CARTESIAN_POINT('Ctrl Pts',(17.5419206392686,20.9630141532614,8.61232139834067));
#186515=CARTESIAN_POINT('Ctrl Pts',(17.6212468240622,21.0144371199192,8.61857368373425));
#186516=CARTESIAN_POINT('Ctrl Pts',(17.7685850356702,21.0965167811082,8.6297108964382));
#186517=CARTESIAN_POINT('Ctrl Pts',(17.8352936637507,21.1292095187879,8.63459302604559));
#186518=CARTESIAN_POINT('Ctrl Pts',(17.9424467809842,21.1749036002337,8.64206172980219));
#186519=CARTESIAN_POINT('Ctrl Pts',(17.9817987944551,21.1903099172229,8.64472884379296));
#186520=CARTESIAN_POINT('Ctrl Pts',(18.0286043463597,21.2070364428942,8.64779172992458));
#186521=CARTESIAN_POINT('Ctrl Pts',(18.0356335873533,21.209506659228,8.64824884936479));
#186522=CARTESIAN_POINT('Ctrl Pts',(18.0470291418612,21.2134438203127,8.64898512079277));
#186523=CARTESIAN_POINT('Ctrl Pts',(18.0513873874888,21.2149336904217,8.6492655787132));
#186524=CARTESIAN_POINT('Ctrl Pts',(18.0591363508275,21.2175544673072,8.64976218403288));
#186525=CARTESIAN_POINT('Ctrl Pts',(18.0625251002234,21.2186910207715,8.64997866165255));
#186526=CARTESIAN_POINT('Ctrl Pts',(18.0698013087,21.221110906632,8.65044197371743));
#186527=CARTESIAN_POINT('Ctrl Pts',(18.0736896053987,21.2223915436632,8.65068864872613));
#186528=CARTESIAN_POINT('Ctrl Pts',(18.0843955130379,21.2258832170086,8.6513653919139));
#186529=CARTESIAN_POINT('Ctrl Pts',(18.0912207483391,21.228070946854,8.65179410929906));
#186530=CARTESIAN_POINT('Ctrl Pts',(18.1280704630463,21.2396765514499,8.65409479170168));
#186531=CARTESIAN_POINT('Ctrl Pts',(18.1582927002294,21.2484593241625,8.65593179515854));
#186532=CARTESIAN_POINT('Ctrl Pts',(18.3467774085552,21.298704827258,8.66714516511271));
#186533=CARTESIAN_POINT('Ctrl Pts',(18.5092219756294,21.3223834013349,8.67579050159908));
#186534=CARTESIAN_POINT('Ctrl Pts',(18.7898605182821,21.3305014015687,8.69115899752462));
#186535=CARTESIAN_POINT('Ctrl Pts',(18.9069971212944,21.3241666512854,8.69769646181053));
#186536=CARTESIAN_POINT('Ctrl Pts',(19.037160292131,21.3062296169909,8.7053938810828));
#186537=CARTESIAN_POINT('Ctrl Pts',(19.0512998105927,21.3041349994487,8.7062356112971));
#186538=CARTESIAN_POINT('Ctrl Pts',(19.0737683370982,21.3005736354431,8.70758248036757));
#186539=CARTESIAN_POINT('Ctrl Pts',(19.0821117931145,21.299199865234,8.70808467602384));
#186540=CARTESIAN_POINT('Ctrl Pts',(19.0968115301044,21.2966889716874,8.70897316419808));
#186541=CARTESIAN_POINT('Ctrl Pts',(19.1031712938687,21.2955726773977,8.70935879032419));
#186542=CARTESIAN_POINT('Ctrl Pts',(19.1163141392255,21.2932037550712,8.71015829004696));
#186543=CARTESIAN_POINT('Ctrl Pts',(19.1230963971161,21.2919470369723,8.71057228981612));
#186544=CARTESIAN_POINT('Ctrl Pts',(19.140488597262,21.2886363515486,8.71163765246111));
#186545=CARTESIAN_POINT('Ctrl Pts',(19.1510890764613,21.2865342648327,8.71229054402126));
#186546=CARTESIAN_POINT('Ctrl Pts',(19.1952560094763,21.2774238939222,8.71502598067293));
#186547=CARTESIAN_POINT('Ctrl Pts',(19.2286642503852,21.2696820733236,8.717131843797));
#186548=CARTESIAN_POINT('Ctrl Pts',(19.3152006953957,21.2474006645485,8.72268611991857));
#186549=CARTESIAN_POINT('Ctrl Pts',(19.3679729777837,21.2315938134161,8.72617291489086));
#186550=CARTESIAN_POINT('Ctrl Pts',(19.523531182944,21.1783054790676,8.7367418925451));
#186551=CARTESIAN_POINT('Ctrl Pts',(19.6240874605982,21.1348999929048,8.74397246793019));
#186552=CARTESIAN_POINT('Ctrl Pts',(19.7612298644618,21.0626405847473,8.75421235438756));
#186553=CARTESIAN_POINT('Ctrl Pts',(19.8009293902062,21.0400532841605,8.75722312466314));
#186554=CARTESIAN_POINT('Ctrl Pts',(19.8593541487939,21.0042621778817,8.7616985698565));
#186555=CARTESIAN_POINT('Ctrl Pts',(19.878646074205,20.9920099989053,8.76318389081542));
#186556=CARTESIAN_POINT('Ctrl Pts',(19.8983376726445,20.9790518381292,8.76470519208233));
#186557=CARTESIAN_POINT('Ctrl Pts',(19.8989388408954,20.9786557965923,8.76475164120195));
#186558=CARTESIAN_POINT('Ctrl Pts',(19.9093096320504,20.9718160708575,8.76555302357388));
#186559=CARTESIAN_POINT('Ctrl Pts',(19.9190260227094,20.9652916807653,8.76630515239283));
#186560=CARTESIAN_POINT('Ctrl Pts',(19.9615144178983,20.9362473632967,8.76959831909168));
#186561=CARTESIAN_POINT('Ctrl Pts',(19.9937046455668,20.912885655489,8.77210452662167));
#186562=CARTESIAN_POINT('Ctrl Pts',(20.0310177805011,20.8841668794075,8.77500517654869));
#186563=CARTESIAN_POINT('Ctrl Pts',(20.0367926069563,20.8796743109737,8.77545396810254));
#186564=CARTESIAN_POINT('Ctrl Pts',(20.0461328811133,20.8723299324777,8.77617947322858));
#186565=CARTESIAN_POINT('Ctrl Pts',(20.0497125418777,20.8694964125053,8.77645743264842));
#186566=CARTESIAN_POINT('Ctrl Pts',(20.0560753336055,20.864426309135,8.77695129648943));
#186567=CARTESIAN_POINT('Ctrl Pts',(20.0588619932381,20.8621942487141,8.7771675172768));
#186568=CARTESIAN_POINT('Ctrl Pts',(20.0648524964655,20.8573710427763,8.77763216412739));
#186569=CARTESIAN_POINT('Ctrl Pts',(20.0680544164151,20.8547775982625,8.77788042082209));
#186570=CARTESIAN_POINT('Ctrl Pts',(20.0768991123255,20.8475708346685,8.77856597875068));
#186571=CARTESIAN_POINT('Ctrl Pts',(20.0825257287828,20.8429376474286,8.77900187019559));
#186572=CARTESIAN_POINT('Ctrl Pts',(20.1136733879469,20.817018292085,8.78141429106097));
#186573=CARTESIAN_POINT('Ctrl Pts',(20.1387159212892,20.7951612514057,8.78335171941658));
#186574=CARTESIAN_POINT('Ctrl Pts',(20.2828169990551,20.6632848617021,8.79455868187381));
#186575=CARTESIAN_POINT('Ctrl Pts',(20.389446226444,20.5404641003221,8.80312774843457));
#186576=CARTESIAN_POINT('Ctrl Pts',(20.5468965738085,20.3104089037244,8.81839031467752));
#186577=CARTESIAN_POINT('Ctrl Pts',(20.6046978678858,20.2088868522372,8.82490242911166));
#186578=CARTESIAN_POINT('Ctrl Pts',(20.6598628768075,20.0901730826768,8.83257131253773));
#186579=CARTESIAN_POINT('Ctrl Pts',(20.6657523261035,20.0771559127899,8.8334126748036));
#186580=CARTESIAN_POINT('Ctrl Pts',(20.6749161301474,20.0563431525228,8.83475906508666));
#186581=CARTESIAN_POINT('Ctrl Pts',(20.6782763867676,20.0485856962002,8.83526115321533));
#186582=CARTESIAN_POINT('Ctrl Pts',(20.684120912583,20.0348683847638,8.83614951613709));
#186583=CARTESIAN_POINT('Ctrl Pts',(20.6866245632216,20.0289168678936,8.83653512514127));
#186584=CARTESIAN_POINT('Ctrl Pts',(20.6917467682554,20.0165831306335,8.83733465319021));
#186585=CARTESIAN_POINT('Ctrl Pts',(20.6943614284052,20.0101993851627,8.83774869872205));
#186586=CARTESIAN_POINT('Ctrl Pts',(20.7009932023591,19.9937794097391,8.83881431357548));
#186587=CARTESIAN_POINT('Ctrl Pts',(20.7049646915113,19.9837250743088,8.83946741297881));
#186588=CARTESIAN_POINT('Ctrl Pts',(20.7212224979436,19.9416254777837,8.84220486402173));
#186589=CARTESIAN_POINT('Ctrl Pts',(20.7328050882426,19.9093157221215,8.84431257666857));
#186590=CARTESIAN_POINT('Ctrl Pts',(20.7609359556144,19.824400157788,8.84987289449645));
#186591=CARTESIAN_POINT('Ctrl Pts',(20.7762224790125,19.7714066788445,8.85336398583704));
#186592=CARTESIAN_POINT('Ctrl Pts',(20.8156217323103,19.6116409701314,8.86394121614207));
#186593=CARTESIAN_POINT('Ctrl Pts',(20.8335429627489,19.5035373580111,8.8711757202685));
#186594=CARTESIAN_POINT('Ctrl Pts',(20.8474041199237,19.3442635919094,8.88173661362823));
#186595=CARTESIAN_POINT('Ctrl Pts',(20.8499805205521,19.2938424506443,8.88506354649273));
#186596=CARTESIAN_POINT('Ctrl Pts',(20.8509988449089,19.2272645826091,8.88940321332845));
#186597=CARTESIAN_POINT('Ctrl Pts',(20.8510613222928,19.2111503441033,8.89044940917388));
#186598=CARTESIAN_POINT('Ctrl Pts',(20.8505413610625,19.1421968553651,8.89490447670405));
#186599=CARTESIAN_POINT('Ctrl Pts',(20.8481646395735,19.0893854716826,8.89826254618084));
#186600=CARTESIAN_POINT('Ctrl Pts',(20.8430978029372,19.0280490469424,8.90205894433047));
#186601=CARTESIAN_POINT('Ctrl Pts',(20.842328628064,19.0193884251656,8.9025925639966));
#186602=CARTESIAN_POINT('Ctrl Pts',(20.8410825189931,19.0062750441389,8.90339660857446));
#186603=CARTESIAN_POINT('Ctrl Pts',(20.8406447887768,19.0018187767251,8.90366915550236));
#186604=CARTESIAN_POINT('Ctrl Pts',(20.8398333041824,18.9938185231043,8.90415717641673));
#186605=CARTESIAN_POINT('Ctrl Pts',(20.839464738958,18.9902740783354,8.90437293664061));
#186606=CARTESIAN_POINT('Ctrl Pts',(20.8386439729184,18.9825700255041,8.90484091398196));
#186607=CARTESIAN_POINT('Ctrl Pts',(20.8381883915918,18.9784108356438,8.90509293856372));
#186608=CARTESIAN_POINT('Ctrl Pts',(20.8368728095645,18.9667206488736,8.9057996187306));
#186609=CARTESIAN_POINT('Ctrl Pts',(20.8359846785952,18.9591927930324,8.90625271857221));
#186610=CARTESIAN_POINT('Ctrl Pts',(20.8304053367159,18.9139897748609,8.90896253630085));
#186611=CARTESIAN_POINT('Ctrl Pts',(20.8247414451538,18.8764390597623,8.9111679320323));
#186612=CARTESIAN_POINT('Ctrl Pts',(20.8026836505075,18.752844381319,8.91833491903559));
#186613=CARTESIAN_POINT('Ctrl Pts',(20.7819608713346,18.6676609568276,8.92312829340249));
#186614=CARTESIAN_POINT('Ctrl Pts',(20.7042885988098,18.4171746002083,8.93739582605823));
#186615=CARTESIAN_POINT('Ctrl Pts',(20.6321197415067,18.2574117042414,8.94678989527399));
#186616=CARTESIAN_POINT('Ctrl Pts',(20.5291465987849,18.0886501645176,8.95827704152751));
#186617=CARTESIAN_POINT('Ctrl Pts',(20.5168185540834,18.0691688364069,8.95962758848565));
#186618=CARTESIAN_POINT('Ctrl Pts',(20.4989337854135,18.0419024599577,8.96155461648782));
#186619=CARTESIAN_POINT('Ctrl Pts',(20.4936384184402,18.0339473432233,8.96212135021274));
#186620=CARTESIAN_POINT('Ctrl Pts',(20.4849485019721,18.0210823688148,8.96304535197681));
#186621=CARTESIAN_POINT('Ctrl Pts',(20.481586691658,18.0161504782693,8.9634013803295));
#186622=CARTESIAN_POINT('Ctrl Pts',(20.4745072955408,18.00585855428,8.96414816604074));
#186623=CARTESIAN_POINT('Ctrl Pts',(20.4707857079106,18.0005013616934,8.96453907332771));
#186624=CARTESIAN_POINT('Ctrl Pts',(20.4618756257479,17.987801053287,8.96547106243703));
#186625=CARTESIAN_POINT('Ctrl Pts',(20.4566650238094,17.9804736682464,8.96601298864685));
#186626=CARTESIAN_POINT('Ctrl Pts',(20.4389645798133,17.9559152686154,8.96784371992947));
#186627=CARTESIAN_POINT('Ctrl Pts',(20.4262619453185,17.9388398851153,8.96914073630141));
#186628=CARTESIAN_POINT('Ctrl Pts',(20.3163310565787,17.7956268458123,8.9802292688884));
#186629=CARTESIAN_POINT('Ctrl Pts',(20.2054297812672,17.6806637677722,8.99059332796988));
#186630=CARTESIAN_POINT('Ctrl Pts',(19.9812007735863,17.4953294479985,9.00980967430905));
#186631=CARTESIAN_POINT('Ctrl Pts',(19.8720662794367,17.4210708213553,9.01855491827325));
#186632=CARTESIAN_POINT('Ctrl Pts',(19.7429111980303,17.3498078320537,9.02775812765303));
#186633=CARTESIAN_POINT('Ctrl Pts',(19.729007194783,17.3423376956487,9.02873471550535));
#186634=CARTESIAN_POINT('Ctrl Pts',(19.7098769976273,17.3323337774844,9.03005777381811));
#186635=CARTESIAN_POINT('Ctrl Pts',(19.7047223986525,17.3296651768764,9.03041224398883));
#186636=CARTESIAN_POINT('Ctrl Pts',(19.6965187462765,17.3254607356707,9.03097310171822));
#186637=CARTESIAN_POINT('Ctrl Pts',(19.6934768856401,17.3239110353334,9.03118034924952));
#186638=CARTESIAN_POINT('Ctrl Pts',(19.6871908520463,17.3207276935028,9.03160713364915));
#186639=CARTESIAN_POINT('Ctrl Pts',(19.6839462220329,17.3190950424166,9.03182660278023));
#186640=CARTESIAN_POINT('Ctrl Pts',(19.6762115503046,17.3152279812235,9.03234785992133));
#186641=CARTESIAN_POINT('Ctrl Pts',(19.6717177050944,17.3130011434581,9.03264917479978));
#186642=CARTESIAN_POINT('Ctrl Pts',(19.6565657351984,17.3055598281373,9.03366010467592));
#186643=CARTESIAN_POINT('Ctrl Pts',(19.6458714741732,17.300418880699,9.03436528884837));
#186644=CARTESIAN_POINT('Ctrl Pts',(19.5223241343228,17.242300858796,9.04242297514951));
#186645=CARTESIAN_POINT('Ctrl Pts',(19.4050297579828,17.1992944630783,9.04922979631553));
#186646=CARTESIAN_POINT('Ctrl Pts',(19.1220702337999,17.1230753835632,9.06515897295743));
#186647=CARTESIAN_POINT('Ctrl Pts',(18.9549014802433,17.0988391837974,9.07424240420731));
#186648=CARTESIAN_POINT('Ctrl Pts',(18.7631944423158,17.0940714720116,9.08538062365513));
#186649=CARTESIAN_POINT('Ctrl Pts',(18.7397484958448,17.0938779916243,9.0867537966696));
#186650=CARTESIAN_POINT('Ctrl Pts',(18.7066838299938,17.0941543757055,9.08870762755243));
#186651=CARTESIAN_POINT('Ctrl Pts',(18.6970636066579,17.0943003830393,9.08927816178767));
#186652=CARTESIAN_POINT('Ctrl Pts',(18.6814657282565,17.0946434805853,9.09020667340948));
#186653=CARTESIAN_POINT('Ctrl Pts',(18.6754872567324,17.0948003343914,9.09056338664541));
#186654=CARTESIAN_POINT('Ctrl Pts',(18.6629994987755,17.0951809270853,9.09131024509307));
#186655=CARTESIAN_POINT('Ctrl Pts',(18.656490428226,17.0954093767234,9.09170053421352));
#186656=CARTESIAN_POINT('Ctrl Pts',(18.641053696506,17.0960224976979,9.09262854922548));
#186657=CARTESIAN_POINT('Ctrl Pts',(18.6321272656718,17.0964336631945,9.09316710043475));
#186658=CARTESIAN_POINT('Ctrl Pts',(18.6022753854696,17.0979981476717,9.09497469118979));
#186659=CARTESIAN_POINT('Ctrl Pts',(18.5813650193629,17.0994056461668,9.09625166208203));
#186660=CARTESIAN_POINT('Ctrl Pts',(18.4689977468757,17.1086469529097,9.10317411768674));
#186661=CARTESIAN_POINT('Ctrl Pts',(18.3781139811271,17.1221113341864,9.1089947447229));
#186662=CARTESIAN_POINT('Ctrl Pts',(18.1513559762775,17.1709346404093,9.1240412595165));
#186663=CARTESIAN_POINT('Ctrl Pts',(18.0175919036499,17.2139780693049,9.13342403371388));
#186664=CARTESIAN_POINT('Ctrl Pts',(17.8259582696312,17.2973943028361,9.14705017370816));
#186665=CARTESIAN_POINT('Ctrl Pts',(17.7642184589406,17.3279300828075,9.15146497331408));
#186666=CARTESIAN_POINT('Ctrl Pts',(17.6959109174147,17.3659668614466,9.15629247252829));
#186667=CARTESIAN_POINT('Ctrl Pts',(17.6877812076023,17.3705645972942,9.15686605679635));
#186668=CARTESIAN_POINT('Ctrl Pts',(17.6757366186877,17.3774819836445,9.15771410368726));
#186669=CARTESIAN_POINT('Ctrl Pts',(17.6717984876837,17.3797606249721,9.1579911033273));
#186670=CARTESIAN_POINT('Ctrl Pts',(17.6648889400269,17.383788345756,9.15847657074113));
#186671=CARTESIAN_POINT('Ctrl Pts',(17.6619144263182,17.3855320021261,9.15868538407952));
#186672=CARTESIAN_POINT('Ctrl Pts',(17.6555033720541,17.389311229614,9.15913505463748));
#186673=CARTESIAN_POINT('Ctrl Pts',(17.6520683380182,17.3913492554754,9.15937574898482));
#186674=CARTESIAN_POINT('Ctrl Pts',(17.6449785466941,17.395582843679,9.15987208363725));
#186675=CARTESIAN_POINT('Ctrl Pts',(17.6413246092274,17.3977797518398,9.16012763614554));
#186676=CARTESIAN_POINT('Ctrl Pts',(17.6321211229603,17.4033512164634,9.16077075504814));
#186677=CARTESIAN_POINT('Ctrl Pts',(17.6265803770579,17.4067403276081,9.16115741104872));
#186678=CARTESIAN_POINT('Ctrl Pts',(17.6107923423075,17.4164975304387,9.16225793850135));
#186679=CARTESIAN_POINT('Ctrl Pts',(17.6005836022289,17.4229278988107,9.16296806836283));
#186680=CARTESIAN_POINT('Ctrl Pts',(17.5662421936137,17.4449714547255,9.16535381211929));
#186681=CARTESIAN_POINT('Ctrl Pts',(17.5423717695735,17.4609893041071,9.16700694129817));
#186682=CARTESIAN_POINT('Ctrl Pts',(17.4287621384894,17.5406280153867,9.17488717422829));
#186683=CARTESIAN_POINT('Ctrl Pts',(17.3437410750251,17.6106961488667,9.18082889373141));
#186684=CARTESIAN_POINT('Ctrl Pts',(17.1599907382053,17.7878767883132,9.19469283800449));
#186685=CARTESIAN_POINT('Ctrl Pts',(17.0661011901421,17.8991723322635,9.20262350572933));
#186686=CARTESIAN_POINT('Ctrl Pts',(16.9708166169588,18.0390567821129,9.2124484074637));
#186687=CARTESIAN_POINT('Ctrl Pts',(16.9576268383166,18.0591472015648,9.21385537328414));
#186688=CARTESIAN_POINT('Ctrl Pts',(16.9395871698974,18.0876718799658,9.21584932050586));
#186689=CARTESIAN_POINT('Ctrl Pts',(16.9344487309834,18.0959221123655,9.21642560399533));
#186690=CARTESIAN_POINT('Ctrl Pts',(16.9262311968928,18.1093208552034,9.21736094927235));
#186691=CARTESIAN_POINT('Ctrl Pts',(16.9231168153573,18.1144476419223,9.21771870960385));
#186692=CARTESIAN_POINT('Ctrl Pts',(16.9166737686729,18.1251562702191,9.21846574364963));
#186693=CARTESIAN_POINT('Ctrl Pts',(16.9133489375958,18.1307403348829,9.21885515237451));
#186694=CARTESIAN_POINT('Ctrl Pts',(16.9055544185879,18.1439694567169,9.21977741952153));
#186695=CARTESIAN_POINT('Ctrl Pts',(16.9011069111751,18.151627381089,9.22031107575355));
#186696=CARTESIAN_POINT('Ctrl Pts',(16.8865271959018,18.177098074261,9.22208547440209));
#186697=CARTESIAN_POINT('Ctrl Pts',(16.8766058305006,18.1950296231209,9.22333375552151));
#186698=CARTESIAN_POINT('Ctrl Pts',(16.8254558304671,18.2907305574893,9.22999307239614));
#186699=CARTESIAN_POINT('Ctrl Pts',(16.7888520233515,18.3708615246763,9.23556468886471));
#186700=CARTESIAN_POINT('Ctrl Pts',(16.6888533288183,18.6316407808105,9.25364607310298));
#186701=CARTESIAN_POINT('Ctrl Pts',(16.6448918386729,18.8186948884003,9.26662241364255));
#186702=CARTESIAN_POINT('Ctrl Pts',(16.6241532271636,19.0351570266968,9.28035987111827));
#186703=CARTESIAN_POINT('Ctrl Pts',(16.6221401954149,19.0612586674574,9.28199387235902));
#186704=CARTESIAN_POINT('Ctrl Pts',(16.6202046990117,19.094350894635,9.28403146023798));
#186705=CARTESIAN_POINT('Ctrl Pts',(16.6198320670718,19.1013116106487,9.28445814794421));
#186706=CARTESIAN_POINT('Ctrl Pts',(16.6192953239796,19.1123599163827,9.28513224516597));
#186707=CARTESIAN_POINT('Ctrl Pts',(16.6191086720113,19.1164462886426,9.28538088456156));
#186708=CARTESIAN_POINT('Ctrl Pts',(16.6187836663883,19.1240447502766,9.2858419146969));
#186709=CARTESIAN_POINT('Ctrl Pts',(16.6186422162379,19.1275566041032,9.28605447119874));
#186710=CARTESIAN_POINT('Ctrl Pts',(16.6183781735427,19.1345448679932,9.2864764145905));
#186711=CARTESIAN_POINT('Ctrl Pts',(16.6182554037768,19.1380212103176,9.28668580992454));
#186712=CARTESIAN_POINT('Ctrl Pts',(16.6179937476174,19.145986829088,9.28716449546407));
#186713=CARTESIAN_POINT('Ctrl Pts',(16.617860577756,19.1504762941652,9.28743347133359));
#186714=CARTESIAN_POINT('Ctrl Pts',(16.6175253050956,19.1631387138012,9.28818990071531));
#186715=CARTESIAN_POINT('Ctrl Pts',(16.6173562536601,19.1713125623867,9.28867559512321));
#186716=CARTESIAN_POINT('Ctrl Pts',(16.6170813859026,19.1897759473539,9.28976724649768));
#186717=CARTESIAN_POINT('Ctrl Pts',(16.6170032290323,19.2000657276411,9.29037180813144));
#186718=CARTESIAN_POINT('Ctrl Pts',(16.6170000979998,19.2103558486173,9.29097292758594));
#186719=CARTESIAN_POINT('Ctrl Pts',(16.6170000985829,19.2103539350032,9.29097281579803));
#186720=CARTESIAN_POINT('Ctrl Pts',(16.6169387584115,19.411350951311,9.3027144953519));
#186721=CARTESIAN_POINT('Ctrl Pts',(16.6455016513076,19.6113762936101,9.31315911815543));
#186722=CARTESIAN_POINT('Ctrl Pts',(16.7149256836481,19.8491205389225,9.32683326560889));
#186723=CARTESIAN_POINT('Ctrl Pts',(16.7294513745603,19.8933790755415,9.32943087882338));
#186724=CARTESIAN_POINT('Ctrl Pts',(16.7454193811439,19.9371102686989,9.33206801830577));
#186725=CARTESIAN_POINT('Origin',(18.734,19.211,0.));
#186726=CARTESIAN_POINT('',(16.7454193623258,19.9371102171621,10.3555828633409));
#186727=CARTESIAN_POINT('',(16.74541937607,19.9371102548029,10.1325348912934));
#186728=CARTESIAN_POINT('',(16.7454193623258,19.9371102171621,0.));
#186729=CARTESIAN_POINT('',(16.6146463426453,19.2099228989265,10.3109437268626));
#186730=CARTESIAN_POINT('Ctrl Pts',(16.6170002731508,19.2099245836057,10.3109437563774));
#186731=CARTESIAN_POINT('Ctrl Pts',(16.6169638477094,19.28162950639,10.3152783077146));
#186732=CARTESIAN_POINT('Ctrl Pts',(16.6205747319164,19.353482380977,10.3196128590518));
#186733=CARTESIAN_POINT('Ctrl Pts',(16.6278517403654,19.4250759408207,10.3239474103889));
#186734=CARTESIAN_POINT('Ctrl Pts',(16.6351199717677,19.4965831492434,10.3282767336767));
#186735=CARTESIAN_POINT('Ctrl Pts',(16.646045514733,19.5678311749636,10.3326060569645));
#186736=CARTESIAN_POINT('Ctrl Pts',(16.6605951836038,19.6384125259569,10.3369353802523));
#186737=CARTESIAN_POINT('Ctrl Pts',(16.6751308912189,19.7089261500286,10.341260549302));
#186738=CARTESIAN_POINT('Ctrl Pts',(16.6932837245209,19.7787738865221,10.3455857183516));
#186739=CARTESIAN_POINT('Ctrl Pts',(16.7149688972743,19.8475551085539,10.3499108874013));
#186740=CARTESIAN_POINT('Ctrl Pts',(16.7244481243049,19.877621404382,10.3518015460478));
#186741=CARTESIAN_POINT('Ctrl Pts',(16.7346016565717,19.9074840258511,10.3536922046944));
#186742=CARTESIAN_POINT('Ctrl Pts',(16.7454193623258,19.9371102171621,10.3555828633409));
#186743=CARTESIAN_POINT('Ctrl Pts',(16.7437494103711,19.9377357416701,9.55561790998273));
#186744=CARTESIAN_POINT('Ctrl Pts',(16.9543731788316,20.4984180339644,9.59172752395545));
#186745=CARTESIAN_POINT('Ctrl Pts',(17.9482900406235,21.5302730916103,9.67022907348861));
#186746=CARTESIAN_POINT('Ctrl Pts',(20.2082247613025,21.2341144439156,9.79112255858232));
#186747=CARTESIAN_POINT('Ctrl Pts',(21.2330889849398,19.0664837539622,9.91829836526373));
#186748=CARTESIAN_POINT('Ctrl Pts',(19.9651941758505,17.0314377500589,10.0454741719452));
#186749=CARTESIAN_POINT('Ctrl Pts',(17.5677551269472,16.9960048315866,10.1726499786266));
#186750=CARTESIAN_POINT('Ctrl Pts',(16.6440836776345,18.3853146100795,10.2611398283041));
#186751=CARTESIAN_POINT('Ctrl Pts',(16.6137958787386,19.1485339243465,10.307237742421));
#186752=CARTESIAN_POINT('Ctrl Pts',(16.6141769831468,19.2099225630116,10.3109437209775));
#186753=CARTESIAN_POINT('Ctrl Pts',(16.7454193811439,19.9371102686989,9.33206801830577));
#186754=CARTESIAN_POINT('Ctrl Pts',(16.7596281007385,19.9760233451594,9.33441460898639));
#186755=CARTESIAN_POINT('Ctrl Pts',(16.7749788270604,20.0145188815229,9.33679243678394));
#186756=CARTESIAN_POINT('Ctrl Pts',(16.799600250514,20.0713526206786,9.34040242819754));
#186757=CARTESIAN_POINT('Ctrl Pts',(16.8080196105005,20.0900384055731,9.34160574272052));
#186758=CARTESIAN_POINT('Ctrl Pts',(16.8204636459809,20.1166191537079,9.34334235730709));
#186759=CARTESIAN_POINT('Ctrl Pts',(16.8242688215022,20.1246160309219,9.34386808618027));
#186760=CARTESIAN_POINT('Ctrl Pts',(16.8309532210406,20.1384395906669,9.34478264772074));
#186761=CARTESIAN_POINT('Ctrl Pts',(16.833809326711,20.1442773654905,9.34517067219684));
#186762=CARTESIAN_POINT('Ctrl Pts',(16.8393532075784,20.1554779058867,9.34591865544923));
#186763=CARTESIAN_POINT('Ctrl Pts',(16.8420369875027,20.1608425874493,9.3462784715275));
#186764=CARTESIAN_POINT('Ctrl Pts',(16.8491288389102,20.1748693734016,9.3472233930721));
#186765=CARTESIAN_POINT('Ctrl Pts',(16.8535737882089,20.1835125808802,9.34780979147014));
#186766=CARTESIAN_POINT('Ctrl Pts',(16.8692147876912,20.2134183538443,9.34985337542285));
#186767=CARTESIAN_POINT('Ctrl Pts',(16.8807129028743,20.234520056051,9.35132121027353));
#186768=CARTESIAN_POINT('Ctrl Pts',(16.9644481534212,20.3821548241038,9.36177890161196));
#186769=CARTESIAN_POINT('Ctrl Pts',(17.0492075563428,20.5011077237472,9.3712345550802));
#186770=CARTESIAN_POINT('Ctrl Pts',(17.2361105315342,20.713268522094,9.38989437635894));
#186771=CARTESIAN_POINT('Ctrl Pts',(17.336517670782,20.8070990942191,9.39902731688534));
#186772=CARTESIAN_POINT('Ctrl Pts',(17.4553852073467,20.898304007343,9.40841002993629));
#186773=CARTESIAN_POINT('Ctrl Pts',(17.4655404945254,20.9059516515597,9.40920105765478));
#186774=CARTESIAN_POINT('Ctrl Pts',(17.4811848239039,20.9175135700109,9.410402799992));
#186775=CARTESIAN_POINT('Ctrl Pts',(17.4866245144744,20.9214937389326,9.41081758410069));
#186776=CARTESIAN_POINT('Ctrl Pts',(17.4956182803278,20.9280086693425,9.41149819785481));
#186777=CARTESIAN_POINT('Ctrl Pts',(17.4991613057385,20.9305585055886,9.41176500808274));
#186778=CARTESIAN_POINT('Ctrl Pts',(17.5060249205051,20.9354659428674,9.41227930598831));
#186779=CARTESIAN_POINT('Ctrl Pts',(17.5093444726057,20.9378249546025,9.41252688810126));
#186780=CARTESIAN_POINT('Ctrl Pts',(17.5126805298925,20.940181237487,9.41277452751432));
#186781=CARTESIAN_POINT('Ctrl Pts',(17.5126902162028,20.9401880788803,9.41277524653049));
#186782=CARTESIAN_POINT('Ctrl Pts',(17.5127096231875,20.9402017856938,9.41277668709386));
#186783=CARTESIAN_POINT('Ctrl Pts',(17.5127193439062,20.9402086511444,9.41277740864427));
#186784=CARTESIAN_POINT('Ctrl Pts',(17.5127388197587,20.9402224061058,9.41277885427966));
#186785=CARTESIAN_POINT('Ctrl Pts',(17.5127485751299,20.9402292957833,9.4127795783822));
#186786=CARTESIAN_POINT('Ctrl Pts',(17.5127687274431,20.9402435279888,9.41278107418778));
#186787=CARTESIAN_POINT('Ctrl Pts',(17.5127791240243,20.940250870245,9.41278184586269));
#186788=CARTESIAN_POINT('Ctrl Pts',(17.5128000847218,20.9402656727906,9.4127834016246));
#186789=CARTESIAN_POINT('Ctrl Pts',(17.5128106488415,20.9402731330777,9.41278418571149));
#186790=CARTESIAN_POINT('Ctrl Pts',(17.5128319477846,20.9402881739089,9.41278576653144));
#186791=CARTESIAN_POINT('Ctrl Pts',(17.5128426830051,20.9402957547286,9.41278656329358));
#186792=CARTESIAN_POINT('Ctrl Pts',(17.5128643283085,20.9403110395475,9.41278816977154));
#186793=CARTESIAN_POINT('Ctrl Pts',(17.512875237834,20.9403187431481,9.41278897944558));
#186794=CARTESIAN_POINT('Ctrl Pts',(17.5128972351988,20.940334275951,9.41279061200228));
#186795=CARTESIAN_POINT('Ctrl Pts',(17.5129083234166,20.9403421054155,9.41279143491261));
#186796=CARTESIAN_POINT('Ctrl Pts',(17.5129306815463,20.9403578923176,9.4127930941915));
#186797=CARTESIAN_POINT('Ctrl Pts',(17.5129419520928,20.9403658501981,9.41279393060673));
#186798=CARTESIAN_POINT('Ctrl Pts',(17.5129646793556,20.9403818970764,9.41279561722627));
#186799=CARTESIAN_POINT('Ctrl Pts',(17.5129761358252,20.9403899858945,9.41279646741182));
#186800=CARTESIAN_POINT('Ctrl Pts',(17.5129992393282,20.940406297734,9.41279818189675));
#186801=CARTESIAN_POINT('Ctrl Pts',(17.5130108860964,20.9404145205624,9.41279904617598));
#186802=CARTESIAN_POINT('Ctrl Pts',(17.5130343743115,20.9404311033103,9.4128007891522));
#186803=CARTESIAN_POINT('Ctrl Pts',(17.5130462156395,20.94043946314,9.41280166783989));
#186804=CARTESIAN_POINT('Ctrl Pts',(17.51307009722,20.9404563228699,9.41280343994664));
#186805=CARTESIAN_POINT('Ctrl Pts',(17.5130821374053,20.9404648227167,9.41280433336023));
#186806=CARTESIAN_POINT('Ctrl Pts',(17.513106420893,20.940481965422,9.41280613522834));
#186807=CARTESIAN_POINT('Ctrl Pts',(17.5131186644979,20.9404906084877,9.4128070437048));
#186808=CARTESIAN_POINT('Ctrl Pts',(17.513143359442,20.9405080408711,9.41280887603971));
#186809=CARTESIAN_POINT('Ctrl Pts',(17.513155810855,20.9405168302342,9.41280979990309));
#186810=CARTESIAN_POINT('Ctrl Pts',(17.5131809264171,20.9405345587228,9.41281166338132));
#186811=CARTESIAN_POINT('Ctrl Pts',(17.5131935903392,20.9405434976812,9.41281260297876));
#186812=CARTESIAN_POINT('Ctrl Pts',(17.5132191357901,20.9405615287776,9.41281449828479));
#186813=CARTESIAN_POINT('Ctrl Pts',(17.5132320172368,20.9405706208504,9.41281545398669));
#186814=CARTESIAN_POINT('Ctrl Pts',(17.513258002494,20.9405889615115,9.41281738185281));
#186815=CARTESIAN_POINT('Ctrl Pts',(17.5132711065358,20.9405982102554,9.41281835403357));
#186816=CARTESIAN_POINT('Ctrl Pts',(17.513297542199,20.9406168679175,9.41282031524251));
#186817=CARTESIAN_POINT('Ctrl Pts',(17.5133108738215,20.9406262768286,9.41282130427014));
#186818=CARTESIAN_POINT('Ctrl Pts',(17.5133377700112,20.9406452585875,9.41282329956891));
#186819=CARTESIAN_POINT('Ctrl Pts',(17.5133513346364,20.9406548314683,9.41282430584369));
#186820=CARTESIAN_POINT('Ctrl Pts',(17.5133787024836,20.9406741451311,9.41282633605408));
#186821=CARTESIAN_POINT('Ctrl Pts',(17.5133925054929,20.9406838857544,9.41282735997321));
#186822=CARTESIAN_POINT('Ctrl Pts',(17.513420355744,20.9407035388539,9.41282942588828));
#186823=CARTESIAN_POINT('Ctrl Pts',(17.5134344029478,20.9407134512942,9.41283046788066));
#186824=CARTESIAN_POINT('Ctrl Pts',(17.5134627471682,20.9407334519388,9.41283257035401));
#186825=CARTESIAN_POINT('Ctrl Pts',(17.5134770444489,20.9407435403201,9.4128336308538));
#186826=CARTESIAN_POINT('Ctrl Pts',(17.5135058949749,20.9407638971594,9.41283577079599));
#186827=CARTESIAN_POINT('Ctrl Pts',(17.5135204481435,20.9407741655538,9.41283685023193));
#186828=CARTESIAN_POINT('Ctrl Pts',(17.5135498167024,20.9407948868053,9.41283902850815));
#186829=CARTESIAN_POINT('Ctrl Pts',(17.5135646321264,20.9408053396761,9.41284012735012));
#186830=CARTESIAN_POINT('Ctrl Pts',(17.5135945318045,20.9408264345128,9.4128423449261));
#186831=CARTESIAN_POINT('Ctrl Pts',(17.5136096157503,20.9408370762507,9.41284346363639));
#186832=CARTESIAN_POINT('Ctrl Pts',(17.513640058837,20.9408585532806,9.41284572141851));
#186833=CARTESIAN_POINT('Ctrl Pts',(17.5136554182315,20.9408693887405,9.41284686050826));
#186834=CARTESIAN_POINT('Ctrl Pts',(17.5136864190702,20.9408912580173,9.41284915955498));
#186835=CARTESIAN_POINT('Ctrl Pts',(17.5137020604677,20.9409022917898,9.41285031950756));
#186836=CARTESIAN_POINT('Ctrl Pts',(17.5165618938005,20.9429196206005,9.41306239756386));
#186837=CARTESIAN_POINT('Ctrl Pts',(17.5194109871642,20.9449188691196,9.41327282152059));
#186838=CARTESIAN_POINT('Ctrl Pts',(17.5260570240062,20.9495580669258,9.41376170238612));
#186839=CARTESIAN_POINT('Ctrl Pts',(17.5298576951851,20.9521926073843,9.41403978901974));
#186840=CARTESIAN_POINT('Ctrl Pts',(17.5399926626179,20.9591688851703,9.41477747456173));
#186841=CARTESIAN_POINT('Ctrl Pts',(17.5463420690897,20.963488692114,9.41523562436576));
#186842=CARTESIAN_POINT('Ctrl Pts',(17.591525953381,20.9938711142462,9.41846874397601));
#186843=CARTESIAN_POINT('Ctrl Pts',(17.6311943467449,21.0186771727644,9.42116560175244));
#186844=CARTESIAN_POINT('Ctrl Pts',(17.6796763050525,21.0468040586029,9.42433588769273));
#186845=CARTESIAN_POINT('Ctrl Pts',(17.6877281129654,21.0514048841929,9.42485835628003));
#186846=CARTESIAN_POINT('Ctrl Pts',(17.7985384561741,21.1137599740331,9.43199687768628));
#186847=CARTESIAN_POINT('Ctrl Pts',(17.9059214618201,21.1628896352737,9.43831699960669));
#186848=CARTESIAN_POINT('Ctrl Pts',(18.1043043065165,21.2343175122883,9.44980139837942));
#186849=CARTESIAN_POINT('Ctrl Pts',(18.1937407176716,21.2600115413304,9.45491327822184));
#186850=CARTESIAN_POINT('Ctrl Pts',(18.3325838853385,21.2901748862576,9.46299073782786));
#186851=CARTESIAN_POINT('Ctrl Pts',(18.3809429405163,21.2989303784758,9.46582841130734));
#186852=CARTESIAN_POINT('Ctrl Pts',(18.4416600177764,21.3077536411689,9.46943946885941));
#186853=CARTESIAN_POINT('Ctrl Pts',(18.4537746321943,21.3094070698383,9.47016231597628));
#186854=CARTESIAN_POINT('Ctrl Pts',(18.4730565038001,21.3118687495453,9.47131680140594));
#186855=CARTESIAN_POINT('Ctrl Pts',(18.4802148572275,21.3127454913376,9.47174627272721));
#186856=CARTESIAN_POINT('Ctrl Pts',(18.4937112527438,21.314328549348,9.47255769549362));
#186857=CARTESIAN_POINT('Ctrl Pts',(18.5000482920473,21.31504283833,9.47293939053565));
#186858=CARTESIAN_POINT('Ctrl Pts',(18.5143264170593,21.3165869171924,9.47380101982015));
#186859=CARTESIAN_POINT('Ctrl Pts',(18.5222691317894,21.3174004333495,9.4742814615128));
#186860=CARTESIAN_POINT('Ctrl Pts',(18.5425762963924,21.3193643345392,9.47551277453454));
#186861=CARTESIAN_POINT('Ctrl Pts',(18.5549464838449,21.320450883406,9.47626564132454));
#186862=CARTESIAN_POINT('Ctrl Pts',(18.6291252882684,21.3263092808806,9.48079766067618));
#186863=CARTESIAN_POINT('Ctrl Pts',(18.6911041758201,21.3284727297351,9.48465794720081));
#186864=CARTESIAN_POINT('Ctrl Pts',(18.9003128034564,21.3265867102618,9.49794316495959));
#186865=CARTESIAN_POINT('Ctrl Pts',(19.0469878126794,21.3099035079008,9.50771742881051));
#186866=CARTESIAN_POINT('Ctrl Pts',(19.2612722989046,21.2625587021597,9.52218318720205));
#186867=CARTESIAN_POINT('Ctrl Pts',(19.3309826031314,21.2433686682805,9.52691186885705));
#186868=CARTESIAN_POINT('Ctrl Pts',(19.4316861478351,21.2100164996713,9.53366083424626));
#186869=CARTESIAN_POINT('Ctrl Pts',(19.4635358006561,21.1986143344654,9.5357825793678));
#186870=CARTESIAN_POINT('Ctrl Pts',(19.5019380082488,21.1838187718195,9.53831371588949));
#186871=CARTESIAN_POINT('Ctrl Pts',(19.5087618865754,21.1811489064738,9.53876242815051));
#186872=CARTESIAN_POINT('Ctrl Pts',(19.5194091322563,21.1769192616052,9.53946073766161));
#186873=CARTESIAN_POINT('Ctrl Pts',(19.5232419557631,21.1753836652034,9.53971174804479));
#186874=CARTESIAN_POINT('Ctrl Pts',(19.5303796690615,21.1724997227989,9.54017847255514));
#186875=CARTESIAN_POINT('Ctrl Pts',(19.5336856069989,21.1711542464921,9.54039434929202));
#186876=CARTESIAN_POINT('Ctrl Pts',(19.5412008644859,21.1680734511483,9.54088443992989));
#186877=CARTESIAN_POINT('Ctrl Pts',(19.5454079892703,21.1663329140209,9.5411583342207));
#186878=CARTESIAN_POINT('Ctrl Pts',(19.5582425095303,21.1609745651282,9.54199257027974));
#186879=CARTESIAN_POINT('Ctrl Pts',(19.5668517014783,21.1573130708558,9.54255033142214));
#186880=CARTESIAN_POINT('Ctrl Pts',(19.6398343106918,21.1257005903039,9.5472653374098));
#186881=CARTESIAN_POINT('Ctrl Pts',(19.7028124370688,21.0946185210883,9.55124625427611));
#186882=CARTESIAN_POINT('Ctrl Pts',(19.8992010421097,20.9852315694685,9.56373242246249));
#186883=CARTESIAN_POINT('Ctrl Pts',(20.0256204835678,20.8954320242298,9.57191522153338));
#186884=CARTESIAN_POINT('Ctrl Pts',(20.1997608206408,20.7405068302424,9.58485344076542));
#186885=CARTESIAN_POINT('Ctrl Pts',(20.2554342288704,20.6851376813337,9.58929456876296));
#186886=CARTESIAN_POINT('Ctrl Pts',(20.3207875952805,20.6124868218698,9.5949975322865));
#186887=CARTESIAN_POINT('Ctrl Pts',(20.3334759766611,20.597988373502,9.59612973170588));
#186888=CARTESIAN_POINT('Ctrl Pts',(20.3515639094661,20.5767417817744,9.59778146651719));
#186889=CARTESIAN_POINT('Ctrl Pts',(20.3571230372128,20.5701303169263,9.59829442756405));
#186890=CARTESIAN_POINT('Ctrl Pts',(20.366770155013,20.5585134078847,9.59919405943496));
#186891=CARTESIAN_POINT('Ctrl Pts',(20.3708760028081,20.5535228912506,9.59957999620287));
#186892=CARTESIAN_POINT('Ctrl Pts',(20.3787836918481,20.5438211642618,9.60032927282243));
#186893=CARTESIAN_POINT('Ctrl Pts',(20.3825883054764,20.5391122869457,9.60069249526767));
#186894=CARTESIAN_POINT('Ctrl Pts',(20.3916029334457,20.5278566811168,9.60155967097323));
#186895=CARTESIAN_POINT('Ctrl Pts',(20.3967944075215,20.5212952944819,9.60206436039392));
#186896=CARTESIAN_POINT('Ctrl Pts',(20.4152072233348,20.4977380976677,9.60387352275821));
#186897=CARTESIAN_POINT('Ctrl Pts',(20.4282076401234,20.4805720059056,9.60518668480398));
#186898=CARTESIAN_POINT('Ctrl Pts',(20.5538775553782,20.3092658586791,9.61824486798882));
#186899=CARTESIAN_POINT('Ctrl Pts',(20.6454462374491,20.1407771015906,9.63084302977509));
#186900=CARTESIAN_POINT('Ctrl Pts',(20.7404062532465,19.8906375899434,9.64849732622681));
#186901=CARTESIAN_POINT('Ctrl Pts',(20.763715345848,19.8174903334324,9.65352906561344));
#186902=CARTESIAN_POINT('Ctrl Pts',(20.7918249920106,19.7092735126506,9.66065043991878));
#186903=CARTESIAN_POINT('Ctrl Pts',(20.7998014553974,19.6750957559884,9.66285353592872));
#186904=CARTESIAN_POINT('Ctrl Pts',(20.8084288842392,19.6334792154909,9.66546799988751));
#186905=CARTESIAN_POINT('Ctrl Pts',(20.8098946498099,19.6262171599412,9.66592172557927));
#186906=CARTESIAN_POINT('Ctrl Pts',(20.8121213511723,19.6148785021958,9.6666261033216));
#186907=CARTESIAN_POINT('Ctrl Pts',(20.8129084655181,19.6108071877952,9.66687820808131));
#186908=CARTESIAN_POINT('Ctrl Pts',(20.8143504395285,19.6032292360288,9.66734590698785));
#186909=CARTESIAN_POINT('Ctrl Pts',(20.815008392145,19.599723290952,9.66756167027225));
#186910=CARTESIAN_POINT('Ctrl Pts',(20.8164813800908,19.591763446499,9.66805014862078));
#186911=CARTESIAN_POINT('Ctrl Pts',(20.8172909883079,19.5873085961343,9.66832255253708));
#186912=CARTESIAN_POINT('Ctrl Pts',(20.8196545536143,19.5740616980512,9.66912974932144));
#186913=CARTESIAN_POINT('Ctrl Pts',(20.8211672132267,19.565262253105,9.66966225321033));
#186914=CARTESIAN_POINT('Ctrl Pts',(20.8322368213428,19.4983349740359,9.67368620393002));
#186915=CARTESIAN_POINT('Ctrl Pts',(20.8394203940534,19.439834967184,9.67705377020056));
#186916=CARTESIAN_POINT('Ctrl Pts',(20.8570770517325,19.2208054902046,9.6893566039729));
#186917=CARTESIAN_POINT('Ctrl Pts',(20.8516923482769,19.0595489754792,9.69784431923421));
#186918=CARTESIAN_POINT('Ctrl Pts',(20.8191689273743,18.840237593498,9.71011781427093));
#186919=CARTESIAN_POINT('Ctrl Pts',(20.807647454331,18.7804426573627,9.71353580115989));
#186920=CARTESIAN_POINT('Ctrl Pts',(20.785040255936,18.6853754910086,9.71914553620922));
#186921=CARTESIAN_POINT('Ctrl Pts',(20.775579519628,18.6497513215909,9.72128786260963));
#186922=CARTESIAN_POINT('Ctrl Pts',(20.7620683839582,18.6037515694995,9.72411415973216));
#186923=CARTESIAN_POINT('Ctrl Pts',(20.7588590063686,18.593134299703,9.72477069831319));
#186924=CARTESIAN_POINT('Ctrl Pts',(20.7535000923061,18.5758962091658,9.72584368684579));
#186925=CARTESIAN_POINT('Ctrl Pts',(20.7514010479275,18.5692598204887,9.72625847736569));
#186926=CARTESIAN_POINT('Ctrl Pts',(20.7472988162594,18.5565091499987,9.72705876548025));
#186927=CARTESIAN_POINT('Ctrl Pts',(20.7453004052019,18.5503934038293,9.7274441019859));
#186928=CARTESIAN_POINT('Ctrl Pts',(20.740657039339,18.5363996856014,9.7283292593097));
#186929=CARTESIAN_POINT('Ctrl Pts',(20.7379935272576,18.528528024495,9.72882968907687));
#186930=CARTESIAN_POINT('Ctrl Pts',(20.730785679499,18.5076322246168,9.73016491009954));
#186931=CARTESIAN_POINT('Ctrl Pts',(20.7261603340591,18.4946366378958,9.73100237589546));
#186932=CARTESIAN_POINT('Ctrl Pts',(20.6893635205931,18.3943637260913,9.73752004312335));
#186933=CARTESIAN_POINT('Ctrl Pts',(20.6516026765133,18.309258785791,9.74338782813992));
#186934=CARTESIAN_POINT('Ctrl Pts',(20.5253710009559,18.0688254956185,9.76094443945539));
#186935=CARTESIAN_POINT('Ctrl Pts',(20.4227092916545,17.9218812959764,9.77300970691708));
#186936=CARTESIAN_POINT('Ctrl Pts',(20.2755859673156,17.7595014255634,9.78703159142716));
#186937=CARTESIAN_POINT('Ctrl Pts',(20.2474808402312,17.7302192429143,9.78958854688714));
#186938=CARTESIAN_POINT('Ctrl Pts',(20.2130440612626,17.6963458160479,9.79256190395354));
#186939=CARTESIAN_POINT('Ctrl Pts',(20.2075091221436,17.6909606902144,9.79303508282084));
#186940=CARTESIAN_POINT('Ctrl Pts',(20.198907785184,17.6826832967284,9.79376296659046));
#186941=CARTESIAN_POINT('Ctrl Pts',(20.195862075093,17.6797697629975,9.79401928213883));
#186942=CARTESIAN_POINT('Ctrl Pts',(20.1902268206243,17.6744112032621,9.79449086517782));
#186943=CARTESIAN_POINT('Ctrl Pts',(20.1876398271179,17.671963633726,9.79470632659517));
#186944=CARTESIAN_POINT('Ctrl Pts',(20.1818143231824,17.6664798832497,9.79518921435753));
#186945=CARTESIAN_POINT('Ctrl Pts',(20.1785724426174,17.6634473629906,9.79545635953401));
#186946=CARTESIAN_POINT('Ctrl Pts',(20.1702651323803,17.6557253882091,9.79613696539065));
#186947=CARTESIAN_POINT('Ctrl Pts',(20.165186217024,17.6510504291051,9.79654934360758));
#186948=CARTESIAN_POINT('Ctrl Pts',(20.1356114285308,17.6240939196917,9.79892975153214));
#186949=CARTESIAN_POINT('Ctrl Pts',(20.1106168676723,17.602363379293,9.80085896197606));
#186950=CARTESIAN_POINT('Ctrl Pts',(20.0710799883463,17.569586351999,9.80380386622175));
#186951=CARTESIAN_POINT('Ctrl Pts',(20.0568885109559,17.5581274454272,9.80484044571783));
#186952=CARTESIAN_POINT('Ctrl Pts',(20.0413783741312,17.5459315300434,9.80595355913886));
#186953=CARTESIAN_POINT('Ctrl Pts',(20.0402054192809,17.5450112168902,9.80603761743213));
#186954=CARTESIAN_POINT('Ctrl Pts',(20.0209855025488,17.5299638365166,9.80741302652882));
#186955=CARTESIAN_POINT('Ctrl Pts',(20.0027108115793,17.5161291506381,9.80869251753807));
#186956=CARTESIAN_POINT('Ctrl Pts',(19.9473566218194,17.475620862615,9.81249591811558));
#186957=CARTESIAN_POINT('Ctrl Pts',(19.9096342976774,17.449847173987,9.81499336509444));
#186958=CARTESIAN_POINT('Ctrl Pts',(19.7788703661665,17.3665780558736,9.8234336080593));
#186959=CARTESIAN_POINT('Ctrl Pts',(19.6822226065287,17.3150782202702,9.82932170190214));
#186960=CARTESIAN_POINT('Ctrl Pts',(19.5315380787513,17.2492000250523,9.83846604670764));
#186961=CARTESIAN_POINT('Ctrl Pts',(19.4802031295573,17.2291053577884,9.84157356806095));
#186962=CARTESIAN_POINT('Ctrl Pts',(19.395734245113,17.1997879759382,9.84671758659699));
#186963=CARTESIAN_POINT('Ctrl Pts',(19.3630560511335,17.1893288336569,9.84871469596928));
#186964=CARTESIAN_POINT('Ctrl Pts',(19.319767937637,17.1766249716555,9.85137534020413));
#186965=CARTESIAN_POINT('Ctrl Pts',(19.3093734145566,17.1736607400881,9.8520153468036));
#186966=CARTESIAN_POINT('Ctrl Pts',(19.2923087888241,17.1689353876189,9.85306805391278));
#186967=CARTESIAN_POINT('Ctrl Pts',(19.2856518903108,17.1671270159322,9.85347921313596));
#186968=CARTESIAN_POINT('Ctrl Pts',(19.2727471211575,17.1636890245688,9.85427728154789));
#186969=CARTESIAN_POINT('Ctrl Pts',(19.266500392518,17.162055388447,9.85466405535921));
#186970=CARTESIAN_POINT('Ctrl Pts',(19.2520570036281,17.1583486844274,9.85555943473606));
#186971=CARTESIAN_POINT('Ctrl Pts',(19.2438552437357,17.1562961017398,9.85606869643465));
#186972=CARTESIAN_POINT('Ctrl Pts',(19.2217585237542,17.1509065978905,9.8574430099492));
#186973=CARTESIAN_POINT('Ctrl Pts',(19.2078418939941,17.147661189555,9.85831098986632));
#186974=CARTESIAN_POINT('Ctrl Pts',(19.0798345040287,17.119172721012,9.86631834169499));
#186975=CARTESIAN_POINT('Ctrl Pts',(18.9638883078665,17.1032793287341,9.87375949835684));
#186976=CARTESIAN_POINT('Ctrl Pts',(18.684749178758,17.0883266571225,9.89201886129173));
#186977=CARTESIAN_POINT('Ctrl Pts',(18.521801851443,17.0983855574817,9.90297712302515));
#186978=CARTESIAN_POINT('Ctrl Pts',(18.3296137113565,17.1327272631173,9.91538262512077));
#186979=CARTESIAN_POINT('Ctrl Pts',(18.2977454115203,17.1391824303416,9.91742015081506));
#186980=CARTESIAN_POINT('Ctrl Pts',(18.258975903729,17.1479698205654,9.91986466718118));
#186981=CARTESIAN_POINT('Ctrl Pts',(18.2519234313814,17.1496063940205,9.92030794582583));
#186982=CARTESIAN_POINT('Ctrl Pts',(18.2408808821106,17.1522286612831,9.92099967406839));
#186983=CARTESIAN_POINT('Ctrl Pts',(18.2368851211693,17.1531898320158,9.92124949442663));
#186984=CARTESIAN_POINT('Ctrl Pts',(18.2294217721284,17.1550081298072,9.92171517768832));
#186985=CARTESIAN_POINT('Ctrl Pts',(18.225953592492,17.1558623874812,9.92193119605804));
#186986=CARTESIAN_POINT('Ctrl Pts',(18.2180419452963,17.157832380401,9.92242312320166));
#186987=CARTESIAN_POINT('Ctrl Pts',(18.2135999356597,17.1589537621381,9.9226987028075));
#186988=CARTESIAN_POINT('Ctrl Pts',(18.1999587829063,17.1624446027444,9.92354320179306));
#186989=CARTESIAN_POINT('Ctrl Pts',(18.1907717736573,17.164861603192,9.92410944703244));
#186990=CARTESIAN_POINT('Ctrl Pts',(18.1084454909791,17.187114303175,9.92916368603585));
#186991=CARTESIAN_POINT('Ctrl Pts',(18.0363957230491,17.2108043533015,9.93344589228252));
#186992=CARTESIAN_POINT('Ctrl Pts',(17.9259443271559,17.2538180556921,9.94000667112427));
#186993=CARTESIAN_POINT('Ctrl Pts',(17.8866016881268,17.2705280417435,9.94234269396019));
#186994=CARTESIAN_POINT('Ctrl Pts',(17.7485092341623,17.3341813865009,9.95062116243442));
#186995=CARTESIAN_POINT('Ctrl Pts',(17.652922559694,17.3875661957144,9.95650786140303));
#186996=CARTESIAN_POINT('Ctrl Pts',(17.5160260242026,17.4785849988185,9.96564896340301));
#186997=CARTESIAN_POINT('Ctrl Pts',(17.4713725031269,17.5108548585996,9.96875462608136));
#186998=CARTESIAN_POINT('Ctrl Pts',(17.4010406017053,17.5659820083536,9.97389584213913));
#186999=CARTESIAN_POINT('Ctrl Pts',(17.3745703894922,17.5877884031711,9.9758920639649));
#187000=CARTESIAN_POINT('Ctrl Pts',(17.3404706758821,17.6172993327085,9.97855169331007));
#187001=CARTESIAN_POINT('Ctrl Pts',(17.3323532379288,17.6244338520182,9.97919159547047));
#187002=CARTESIAN_POINT('Ctrl Pts',(17.3191448627516,17.6362233428168,9.98024417455092));
#187003=CARTESIAN_POINT('Ctrl Pts',(17.3140213577778,17.6408416534283,9.98065531092042));
#187004=CARTESIAN_POINT('Ctrl Pts',(17.3041456362576,17.64983146611,9.9814533662518));
#187005=CARTESIAN_POINT('Ctrl Pts',(17.2993906642124,17.6541998378213,9.98184015000184));
#187006=CARTESIAN_POINT('Ctrl Pts',(17.2884551799254,17.664338863289,9.98273559796094));
#187007=CARTESIAN_POINT('Ctrl Pts',(17.2822891391162,17.6701249006464,9.98324491861934));
#187008=CARTESIAN_POINT('Ctrl Pts',(17.2657938264573,17.6857905291081,9.98461949441582));
#187009=CARTESIAN_POINT('Ctrl Pts',(17.2555298120623,17.6957379151518,9.98548767939412));
#187010=CARTESIAN_POINT('Ctrl Pts',(17.1621045915556,17.7881340994369,9.99351084430885));
#187011=CARTESIAN_POINT('Ctrl Pts',(17.085831394973,17.8772328015539,10.0009689933854));
#187012=CARTESIAN_POINT('Ctrl Pts',(16.9216222308105,18.1047806964446,10.0193000846084));
#187013=CARTESIAN_POINT('Ctrl Pts',(16.8416122341248,18.248034232571,10.030315221451));
#187014=CARTESIAN_POINT('Ctrl Pts',(16.766787803809,18.4282095920219,10.0427007555383));
#187015=CARTESIAN_POINT('Ctrl Pts',(16.7553382284952,18.457619293694,10.044677089349));
#187016=CARTESIAN_POINT('Ctrl Pts',(16.7420974934782,18.4940168337103,10.0470584329619));
#187017=CARTESIAN_POINT('Ctrl Pts',(16.7396794444505,18.5007704727776,10.0474975984361));
#187018=CARTESIAN_POINT('Ctrl Pts',(16.735934967577,18.5113987594066,10.0481843418059));
#187019=CARTESIAN_POINT('Ctrl Pts',(16.734585400856,18.5152651144164,10.0484332587459));
#187020=CARTESIAN_POINT('Ctrl Pts',(16.7320789915764,18.5225132172317,10.0488981650053));
#187021=CARTESIAN_POINT('Ctrl Pts',(16.7309195071424,18.5258939400612,10.0491143043344));
#187022=CARTESIAN_POINT('Ctrl Pts',(16.7282860719747,18.5336361149015,10.0496076870388));
#187023=CARTESIAN_POINT('Ctrl Pts',(16.7268177853716,18.5379994412275,10.049884593726));
#187024=CARTESIAN_POINT('Ctrl Pts',(16.722327345533,18.5514891553477,10.0507372239692));
#187025=CARTESIAN_POINT('Ctrl Pts',(16.7193530677122,18.5606315128752,10.0513101980963));
#187026=CARTESIAN_POINT('Ctrl Pts',(16.6905474218074,18.6512686680753,10.0569454327714));
#187027=CARTESIAN_POINT('Ctrl Pts',(16.6696095011782,18.7342474219198,10.0617451522039));
#187028=CARTESIAN_POINT('Ctrl Pts',(16.6294008318276,18.947231259688,10.0736795322587));
#187029=CARTESIAN_POINT('Ctrl Pts',(16.6170990832107,19.0781722139405,10.0806785868332));
#187030=CARTESIAN_POINT('Ctrl Pts',(16.6169313786663,19.3016470690534,10.0930378845873));
#187031=CARTESIAN_POINT('Ctrl Pts',(16.6228899854553,19.3937783351956,10.0982490879101));
#187032=CARTESIAN_POINT('Ctrl Pts',(16.6366195100217,19.4988780731671,10.1044627454843));
#187033=CARTESIAN_POINT('Ctrl Pts',(16.6385368153887,19.5125173847697,10.1052742421342));
#187034=CARTESIAN_POINT('Ctrl Pts',(16.6418231771176,19.5343482615356,10.1065817209942));
#187035=CARTESIAN_POINT('Ctrl Pts',(16.6431076017331,19.5425523070582,10.1070750262759));
#187036=CARTESIAN_POINT('Ctrl Pts',(16.6454726643887,19.5570981838056,10.1079532175542));
#187037=CARTESIAN_POINT('Ctrl Pts',(16.646534009996,19.5634430785184,10.1083374867896));
#187038=CARTESIAN_POINT('Ctrl Pts',(16.6488043602059,19.5766454984752,10.1091396200645));
#187039=CARTESIAN_POINT('Ctrl Pts',(16.6500183105162,19.5835020843766,10.1095576372742));
#187040=CARTESIAN_POINT('Ctrl Pts',(16.6532558815059,19.6012771066016,10.1106450894066));
#187041=CARTESIAN_POINT('Ctrl Pts',(16.6553316014523,19.6121857276935,10.1113161770975));
#187042=CARTESIAN_POINT('Ctrl Pts',(16.6646897605166,19.6593426085278,10.1142336505211));
#187043=CARTESIAN_POINT('Ctrl Pts',(16.6728349140608,19.6954111683336,10.1165074103893));
#187044=CARTESIAN_POINT('Ctrl Pts',(16.6969459037756,19.7905155160465,10.1226194541523));
#187045=CARTESIAN_POINT('Ctrl Pts',(16.7145313850519,19.8491011210258,10.1265064288919));
#187046=CARTESIAN_POINT('Ctrl Pts',(16.7381478917004,19.9169590415021,10.1311462812496));
#187047=CARTESIAN_POINT('Ctrl Pts',(16.7417458056892,19.9270495362942,10.1318398413702));
#187048=CARTESIAN_POINT('Ctrl Pts',(16.74541937607,19.9371102548029,10.1325348912934));
#187049=CARTESIAN_POINT('Origin',(18.734,19.211,0.));
#187050=CARTESIAN_POINT('',(16.745419285258,19.9371100060984,11.1558808557757));
#187051=CARTESIAN_POINT('',(16.7454193623258,19.9371102171621,10.9336112429045));
#187052=CARTESIAN_POINT('',(16.7454193623258,19.9371102171621,0.));
#187053=CARTESIAN_POINT('',(16.6170004031077,19.2096935705332,11.1109437209282));
#187054=CARTESIAN_POINT('Ctrl Pts',(16.745419285258,19.9371100060985,11.1558808557757));
#187055=CARTESIAN_POINT('Ctrl Pts',(16.7234349503207,19.8769020154143,11.1523876679106));
#187056=CARTESIAN_POINT('Ctrl Pts',(16.7041766146871,19.8156728636758,11.148866777791));
#187057=CARTESIAN_POINT('Ctrl Pts',(16.6773854470669,19.7146376045154,11.1430184305134));
#187058=CARTESIAN_POINT('Ctrl Pts',(16.6681681722473,19.6753843801569,11.140737389594));
#187059=CARTESIAN_POINT('Ctrl Pts',(16.6588573166312,19.6299377081226,11.1380746112071));
#187060=CARTESIAN_POINT('Ctrl Pts',(16.6576628084352,19.6239767856912,11.1377249294554));
#187061=CARTESIAN_POINT('Ctrl Pts',(16.6558534143148,19.6147410928009,11.1371824413015));
#187062=CARTESIAN_POINT('Ctrl Pts',(16.6552205500167,19.6114698487589,11.1369901584407));
#187063=CARTESIAN_POINT('Ctrl Pts',(16.649172395059,19.5798065763244,11.1351276415146));
#187064=CARTESIAN_POINT('Ctrl Pts',(16.6443315839102,19.5513090136826,11.1334407179447));
#187065=CARTESIAN_POINT('Ctrl Pts',(16.63853230186,19.5123536407143,11.1311167824628));
#187066=CARTESIAN_POINT('Ctrl Pts',(16.637065784985,19.5019738521413,11.13049584114));
#187067=CARTESIAN_POINT('Ctrl Pts',(16.634862067449,19.4854935228041,11.1295070686686));
#187068=CARTESIAN_POINT('Ctrl Pts',(16.6340742206889,19.4793998399713,11.129140841427));
#187069=CARTESIAN_POINT('Ctrl Pts',(16.63254836061,19.4671797882265,11.128405137446));
#187070=CARTESIAN_POINT('Ctrl Pts',(16.6318105825512,19.4610534513,11.1280356571333));
#187071=CARTESIAN_POINT('Ctrl Pts',(16.6303836083822,19.4487513235021,11.127292384545));
#187072=CARTESIAN_POINT('Ctrl Pts',(16.6296947991948,19.442575550285,11.1269185839524));
#187073=CARTESIAN_POINT('Ctrl Pts',(16.6281826815282,19.4284539820372,11.1260622805929));
#187074=CARTESIAN_POINT('Ctrl Pts',(16.6273771405197,19.4205064157806,11.1255792227055));
#187075=CARTESIAN_POINT('Ctrl Pts',(16.6254321889408,19.4001706885657,11.1243402363105));
#187076=CARTESIAN_POINT('Ctrl Pts',(16.6243569717339,19.3877768258634,11.1235823054178));
#187077=CARTESIAN_POINT('Ctrl Pts',(16.6190952486441,19.320214972957,11.119434868949));
#187078=CARTESIAN_POINT('Ctrl Pts',(16.616963796918,19.264913558275,11.1159819804477));
#187079=CARTESIAN_POINT('Ctrl Pts',(16.6170004651088,19.2095966930235,11.1124693456188));
#187080=CARTESIAN_POINT('Ctrl Pts',(16.7454193623258,19.9371102171621,10.3555828633409));
#187081=CARTESIAN_POINT('Ctrl Pts',(16.7701522519194,20.0048455887312,10.3599055406837));
#187082=CARTESIAN_POINT('Ctrl Pts',(16.7983602447238,20.0713437241127,10.3642282180265));
#187083=CARTESIAN_POINT('Ctrl Pts',(16.8298869170301,20.1362255764207,10.3685508953693));
#187084=CARTESIAN_POINT('Ctrl Pts',(16.8614136510539,20.2011075557432,10.3728735811742));
#187085=CARTESIAN_POINT('Ctrl Pts',(16.8962588589392,20.2643728019858,10.3771962669792));
#187086=CARTESIAN_POINT('Ctrl Pts',(16.9342193458651,20.3256652398822,10.3815189527842));
#187087=CARTESIAN_POINT('Ctrl Pts',(16.972217843787,20.3870190517705,10.3858459670266));
#187088=CARTESIAN_POINT('Ctrl Pts',(17.0133375849194,20.4463956918691,10.390172981269));
#187089=CARTESIAN_POINT('Ctrl Pts',(17.0573316197914,20.5034674629594,10.3944999955115));
#187090=CARTESIAN_POINT('Ctrl Pts',(17.1013502165957,20.5605710973007,10.3988294255321));
#187091=CARTESIAN_POINT('Ctrl Pts',(17.1482459768821,20.6153669278815,10.4031588555527));
#187092=CARTESIAN_POINT('Ctrl Pts',(17.197733021574,20.6675619695014,10.4074882855733));
#187093=CARTESIAN_POINT('Ctrl Pts',(17.2473041635017,20.7198457102697,10.4118250729357));
#187094=CARTESIAN_POINT('Ctrl Pts',(17.2994750180666,20.7695195032584,10.416161860298));
#187095=CARTESIAN_POINT('Ctrl Pts',(17.3539250691498,20.8163293074129,10.4204986476603));
#187096=CARTESIAN_POINT('Ctrl Pts',(17.3811407337521,20.8397261620462,10.42266629577));
#187097=CARTESIAN_POINT('Ctrl Pts',(17.4089253239853,20.862408172781,10.4248339438798));
#187098=CARTESIAN_POINT('Ctrl Pts',(17.4372361998843,20.8843477363386,10.4270015919895));
#187099=CARTESIAN_POINT('Ctrl Pts',(17.494549025663,20.9287624124625,10.4313898009204));
#187100=CARTESIAN_POINT('Ctrl Pts',(17.5542581954977,20.9703158984434,10.4357780098513));
#187101=CARTESIAN_POINT('Ctrl Pts',(17.6160462231312,21.0087397900655,10.4401662187822));
#187102=CARTESIAN_POINT('Ctrl Pts',(17.677742547087,21.0471066542616,10.4445479148834));
#187103=CARTESIAN_POINT('Ctrl Pts',(17.7415111977163,21.0823528921037,10.4489296109847));
#187104=CARTESIAN_POINT('Ctrl Pts',(17.8070029012395,21.1142512653062,10.4533113070859));
#187105=CARTESIAN_POINT('Ctrl Pts',(17.872417646799,21.1461121553816,10.4576878543456));
#187106=CARTESIAN_POINT('Ctrl Pts',(17.9395509916039,21.1746327855722,10.4620644016052));
#187107=CARTESIAN_POINT('Ctrl Pts',(18.0080275301098,21.1996309292982,10.4664409488649));
#187108=CARTESIAN_POINT('Ctrl Pts',(18.0764606417902,21.2246132195648,10.4708147205818));
#187109=CARTESIAN_POINT('Ctrl Pts',(18.1462348050099,21.2460772907211,10.4751884922988));
#187110=CARTESIAN_POINT('Ctrl Pts',(18.2169543269186,21.263888884462,10.4795622640158));
#187111=CARTESIAN_POINT('Ctrl Pts',(18.2876523286393,21.2816950580752,10.4839347047793));
#187112=CARTESIAN_POINT('Ctrl Pts',(18.3592946504356,21.2958508431231,10.4883071455429));
#187113=CARTESIAN_POINT('Ctrl Pts',(18.4314717388384,21.3062722141045,10.4926795863064));
#187114=CARTESIAN_POINT('Ctrl Pts',(18.5036506728174,21.3166938515616,10.4970521388738));
#187115=CARTESIAN_POINT('Ctrl Pts',(18.5763639228389,21.3233808184122,10.5014246914411));
#187116=CARTESIAN_POINT('Ctrl Pts',(18.6491947479435,21.3263007042082,10.5057972440085));
#187117=CARTESIAN_POINT('Ctrl Pts',(18.7221011596255,21.3292236203718,10.5101743345758));
#187118=CARTESIAN_POINT('Ctrl Pts',(18.7951249069976,21.3283716302984,10.5145514251431));
#187119=CARTESIAN_POINT('Ctrl Pts',(18.8678480060379,21.3237644713218,10.5189285157104));
#187120=CARTESIAN_POINT('Ctrl Pts',(18.9406108218616,21.3191547962047,10.5233079967694));
#187121=CARTESIAN_POINT('Ctrl Pts',(19.0130721829179,21.3107859243703,10.5276874778283));
#187122=CARTESIAN_POINT('Ctrl Pts',(19.0848207051465,21.2987293485604,10.5320669588873));
#187123=CARTESIAN_POINT('Ctrl Pts',(19.1566964011491,21.2866514025508,10.536454202547));
#187124=CARTESIAN_POINT('Ctrl Pts',(19.2278562638075,21.2708728040951,10.5408414462067));
#187125=CARTESIAN_POINT('Ctrl Pts',(19.2979011262237,21.2515157484919,10.5452286898664));
#187126=CARTESIAN_POINT('Ctrl Pts',(19.3455248831599,21.2383548159232,10.5482115928013));
#187127=CARTESIAN_POINT('Ctrl Pts',(19.3926335158209,21.2235407241657,10.5511944957361));
#187128=CARTESIAN_POINT('Ctrl Pts',(19.4391069833084,21.2071245307069,10.5541773986709));
#187129=CARTESIAN_POINT('Ctrl Pts',(19.507475042724,21.1829743359732,10.5585656076018));
#187130=CARTESIAN_POINT('Ctrl Pts',(19.5747343896098,21.1552604871605,10.5629538165327));
#187131=CARTESIAN_POINT('Ctrl Pts',(19.6404874892067,21.1241046578564,10.5673420254636));
#187132=CARTESIAN_POINT('Ctrl Pts',(19.7061430003017,21.0929950689686,10.5717237215648));
#187133=CARTESIAN_POINT('Ctrl Pts',(19.7702962696064,21.0584538454433,10.5761054176661));
#187134=CARTESIAN_POINT('Ctrl Pts',(19.8325671704115,21.0206516714811,10.5804871137674));
#187135=CARTESIAN_POINT('Ctrl Pts',(19.8947648979524,20.9828939180816,10.584863661027));
#187136=CARTESIAN_POINT('Ctrl Pts',(19.9550842407134,20.9418830753685,10.5892402082867));
#187137=CARTESIAN_POINT('Ctrl Pts',(20.013168775078,20.8978361642037,10.5936167555463));
#187138=CARTESIAN_POINT('Ctrl Pts',(20.071216473075,20.8538171869499,10.5979905272633));
#187139=CARTESIAN_POINT('Ctrl Pts',(20.1270317913337,20.8067662523015,10.6023642989803));
#187140=CARTESIAN_POINT('Ctrl Pts',(20.1802876588313,20.7569434038516,10.6067380706973));
#187141=CARTESIAN_POINT('Ctrl Pts',(20.2335273203897,20.7071357166618,10.6111105114608));
#187142=CARTESIAN_POINT('Ctrl Pts',(20.2842087253977,20.654558119635,10.6154829522244));
#187143=CARTESIAN_POINT('Ctrl Pts',(20.3320395381811,20.5995095010153,10.6198553929879));
#187144=CARTESIAN_POINT('Ctrl Pts',(20.3798715740037,20.5444594747964,10.6242279455553));
#187145=CARTESIAN_POINT('Ctrl Pts',(20.4248525580104,20.4869386669774,10.6286004981226));
#187146=CARTESIAN_POINT('Ctrl Pts',(20.4667296641662,20.4272799475937,10.63297305069));
#187147=CARTESIAN_POINT('Ctrl Pts',(20.5086502319623,20.3675593121408,10.6373501412573));
#187148=CARTESIAN_POINT('Ctrl Pts',(20.5474602125885,20.3056967307918,10.6417272318247));
#187149=CARTESIAN_POINT('Ctrl Pts',(20.5829499551957,20.2420543454065,10.646104322392));
#187150=CARTESIAN_POINT('Ctrl Pts',(20.6184590800686,20.1783772025526,10.6504838034509));
#187151=CARTESIAN_POINT('Ctrl Pts',(20.6506441436598,20.1129187535676,10.6548632845099));
#187152=CARTESIAN_POINT('Ctrl Pts',(20.6793425856621,20.0460636050083,10.6592427655688));
#187153=CARTESIAN_POINT('Ctrl Pts',(20.7080918954602,19.979089956147,10.6636300092285));
#187154=CARTESIAN_POINT('Ctrl Pts',(20.7333420751798,19.9107151168643,10.6680172528883));
#187155=CARTESIAN_POINT('Ctrl Pts',(20.754979810258,19.8413408653496,10.672404496548));
#187156=CARTESIAN_POINT('Ctrl Pts',(20.7696913851039,19.7941730592069,10.6753873994828));
#187157=CARTESIAN_POINT('Ctrl Pts',(20.7827340876901,19.7465435673451,10.6783703024176));
#187158=CARTESIAN_POINT('Ctrl Pts',(20.794085873422,19.6985809616125,10.6813532053524));
#187159=CARTESIAN_POINT('Ctrl Pts',(20.810785715361,19.6280222007594,10.6857414142833));
#187160=CARTESIAN_POINT('Ctrl Pts',(20.8238889631161,19.5564667533233,10.6901296232142));
#187161=CARTESIAN_POINT('Ctrl Pts',(20.8332827468938,19.4843147427306,10.6945178321451));
#187162=CARTESIAN_POINT('Ctrl Pts',(20.8426625887389,19.4122698176847,10.6988995282463));
#187163=CARTESIAN_POINT('Ctrl Pts',(20.8483438339329,19.3396305615062,10.7032812243476));
#187164=CARTESIAN_POINT('Ctrl Pts',(20.8502642454991,19.266808988722,10.7076629204489));
#187165=CARTESIAN_POINT('Ctrl Pts',(20.8521824004289,19.1940729870813,10.7120394677085));
#187166=CARTESIAN_POINT('Ctrl Pts',(20.8503484880034,19.1211555742339,10.7164160149681));
#187167=CARTESIAN_POINT('Ctrl Pts',(20.8447520630799,19.0484739153125,10.7207925622278));
#187168=CARTESIAN_POINT('Ctrl Pts',(20.8391591873278,18.9758383500428,10.7251663339447));
#187169=CARTESIAN_POINT('Ctrl Pts',(20.8298085704125,18.9034387218193,10.7295401056617));
#187170=CARTESIAN_POINT('Ctrl Pts',(20.8167418305019,18.8316908022767,10.7339138773787));
#187171=CARTESIAN_POINT('Ctrl Pts',(20.8036790668442,18.759964715867,10.7382863181422));
#187172=CARTESIAN_POINT('Ctrl Pts',(20.7869025116119,18.688890418704,10.7426587589058));
#187173=CARTESIAN_POINT('Ctrl Pts',(20.7665052467621,18.6188755013642,10.7470311996693));
#187174=CARTESIAN_POINT('Ctrl Pts',(20.746107460352,18.5488587937354,10.7514037522367));
#187175=CARTESIAN_POINT('Ctrl Pts',(20.7220889173525,18.4799019822769,10.755776304804));
#187176=CARTESIAN_POINT('Ctrl Pts',(20.6945926588479,18.4123978299105,10.7601488573713));
#187177=CARTESIAN_POINT('Ctrl Pts',(20.6670678636891,18.3448236191885,10.7645259479387));
#187178=CARTESIAN_POINT('Ctrl Pts',(20.636058329164,18.278705525327,10.768903038506));
#187179=CARTESIAN_POINT('Ctrl Pts',(20.6017550792379,18.2144158520321,10.7732801290733));
#187180=CARTESIAN_POINT('Ctrl Pts',(20.567433095034,18.1500910677606,10.7776596101322));
#187181=CARTESIAN_POINT('Ctrl Pts',(20.5298140629457,18.0875971057592,10.7820390911912));
#187182=CARTESIAN_POINT('Ctrl Pts',(20.4891333854109,18.0272788337552,10.7864185722501));
#187183=CARTESIAN_POINT('Ctrl Pts',(20.4483806016482,17.9668536480189,10.7908058159098));
#187184=CARTESIAN_POINT('Ctrl Pts',(20.4045556257391,17.9086122391301,10.7951930595695));
#187185=CARTESIAN_POINT('Ctrl Pts',(20.3579349545344,17.8528673616169,10.7995803032293));
#187186=CARTESIAN_POINT('Ctrl Pts',(20.3262373904722,17.8149662164714,10.8025632061641));
#187187=CARTESIAN_POINT('Ctrl Pts',(20.2932482928821,17.7782184270684,10.8055461090989));
#187188=CARTESIAN_POINT('Ctrl Pts',(20.2590638380206,17.7427121229262,10.8085290120338));
#187189=CARTESIAN_POINT('Ctrl Pts',(20.2087743940131,17.6904780796657,10.8129172209647));
#187190=CARTESIAN_POINT('Ctrl Pts',(20.1557001261014,17.6407287153968,10.8173054298956));
#187191=CARTESIAN_POINT('Ctrl Pts',(20.1001163804879,17.5937755149755,10.8216936388264));
#187192=CARTESIAN_POINT('Ctrl Pts',(20.0446151303688,17.5468920008887,10.8260753349277));
#187193=CARTESIAN_POINT('Ctrl Pts',(19.9866121616044,17.5027967211002,10.830457031029));
#187194=CARTESIAN_POINT('Ctrl Pts',(19.926420225514,17.461765022707,10.8348387271302));
#187195=CARTESIAN_POINT('Ctrl Pts',(19.8662990197387,17.4207815398248,10.8392152743899));
#187196=CARTESIAN_POINT('Ctrl Pts',(19.8039943529517,17.3828547573655,10.8435918216495));
#187197=CARTESIAN_POINT('Ctrl Pts',(19.7398513412541,17.3482192616152,10.8479683689092));
#187198=CARTESIAN_POINT('Ctrl Pts',(19.6757490081223,17.3136057311929,10.8523421406261));
#187199=CARTESIAN_POINT('Ctrl Pts',(19.6098110666881,17.2822795746617,10.8567159123431));
#187200=CARTESIAN_POINT('Ctrl Pts',(19.5424096422239,17.2544308470285,10.8610896840601));
#187201=CARTESIAN_POINT('Ctrl Pts',(19.4750287282394,17.2265905938567,10.8654621248236));
#187202=CARTESIAN_POINT('Ctrl Pts',(19.4061856609219,17.202225852836,10.8698345655872));
#187203=CARTESIAN_POINT('Ctrl Pts',(19.3362735429415,17.1814789778195,10.8742070063508));
#187204=CARTESIAN_POINT('Ctrl Pts',(19.2663596373006,17.1607315723031,10.8785795589181));
#187205=CARTESIAN_POINT('Ctrl Pts',(19.1953770897379,17.1436023517757,10.8829521114854));
#187206=CARTESIAN_POINT('Ctrl Pts',(19.1237335771406,17.1301836364424,10.8873246640528));
#187207=CARTESIAN_POINT('Ctrl Pts',(19.0520157102037,17.1167509946602,10.8917017546201));
#187208=CARTESIAN_POINT('Ctrl Pts',(18.9796359837851,17.1070366356522,10.8960788451874));
#187209=CARTESIAN_POINT('Ctrl Pts',(18.9070108440332,17.1010814594286,10.9004559357548));
#187210=CARTESIAN_POINT('Ctrl Pts',(18.8343460409969,17.0951230308623,10.9048354168137));
#187211=CARTESIAN_POINT('Ctrl Pts',(18.7614360402695,17.092927887168,10.9092148978727));
#187212=CARTESIAN_POINT('Ctrl Pts',(18.688698239908,17.0944847625088,10.9135943789316));
#187213=CARTESIAN_POINT('Ctrl Pts',(18.6158315122837,17.0960443974006,10.9179816225913));
#187214=CARTESIAN_POINT('Ctrl Pts',(18.5431380760578,17.1013692966916,10.9223688662511));
#187215=CARTESIAN_POINT('Ctrl Pts',(18.4710305707953,17.110396258381,10.9267561099108));
#187216=CARTESIAN_POINT('Ctrl Pts',(18.4220044154796,17.1165337224938,10.9297390128456));
#187217=CARTESIAN_POINT('Ctrl Pts',(18.373248967218,17.1243814515023,10.9327219157804));
#187218=CARTESIAN_POINT('Ctrl Pts',(18.3248903873722,17.1339062792316,10.9357048187152));
#187219=CARTESIAN_POINT('Ctrl Pts',(18.2537491009803,17.1479184462449,10.9400930276461));
#187220=CARTESIAN_POINT('Ctrl Pts',(18.1831896640502,17.1656171190662,10.944481236577));
#187221=CARTESIAN_POINT('Ctrl Pts',(18.1136230257296,17.1869393759585,10.9488694455079));
#187222=CARTESIAN_POINT('Ctrl Pts',(18.0441596358344,17.2082299870864,10.9532511416092));
#187223=CARTESIAN_POINT('Ctrl Pts',(17.9756865768824,17.2331333660322,10.9576328377104));
#187224=CARTESIAN_POINT('Ctrl Pts',(17.9086046585652,17.2615355785914,10.9620145338117));
#187225=CARTESIAN_POINT('Ctrl Pts',(17.8416015668408,17.2899044162905,10.9663910810714));
#187226=CARTESIAN_POINT('Ctrl Pts',(17.7759868104056,17.3217637331242,10.970767628331));
#187227=CARTESIAN_POINT('Ctrl Pts',(17.7121444440022,17.3569503181747,10.9751441755907));
#187228=CARTESIAN_POINT('Ctrl Pts',(17.6483425654998,17.3921145884043,10.9795179473076));
#187229=CARTESIAN_POINT('Ctrl Pts',(17.5863112682425,17.4306017078622,10.9838917190246));
#187230=CARTESIAN_POINT('Ctrl Pts',(17.5264117827665,17.4722016512549,10.9882654907416));
#187231=CARTESIAN_POINT('Ctrl Pts',(17.466530524905,17.5137889356452,10.9926379315051));
#187232=CARTESIAN_POINT('Ctrl Pts',(17.4087801868836,17.5584868884069,10.9970103722687));
#187233=CARTESIAN_POINT('Ctrl Pts',(17.3534932447844,17.6060420258449,11.0013828130322));
#187234=CARTESIAN_POINT('Ctrl Pts',(17.2982048889917,17.6535983792732,11.0057553655996));
#187235=CARTESIAN_POINT('Ctrl Pts',(17.2453804185809,17.7040117463517,11.0101279181669));
#187236=CARTESIAN_POINT('Ctrl Pts',(17.1953181280009,17.7569893065106,11.0145004707343));
#187237=CARTESIAN_POINT('Ctrl Pts',(17.1452038808876,17.8100218487797,11.0188775613016));
#187238=CARTESIAN_POINT('Ctrl Pts',(17.0978578691722,17.8656235460741,11.0232546518689));
#187239=CARTESIAN_POINT('Ctrl Pts',(17.0535398976922,17.9234663714871,11.0276317424363));
#187240=CARTESIAN_POINT('Ctrl Pts',(17.0091977225231,17.9813407870138,11.0320112234952));
#187241=CARTESIAN_POINT('Ctrl Pts',(16.9678871535191,18.0414583697202,11.0363907045542));
#187242=CARTESIAN_POINT('Ctrl Pts',(16.9298246475457,18.1034620559113,11.0407701856131));
#187243=CARTESIAN_POINT('Ctrl Pts',(16.8916946760359,18.1655756432198,11.0451574292728));
#187244=CARTESIAN_POINT('Ctrl Pts',(16.856824495367,18.2295815860916,11.0495446729326));
#187245=CARTESIAN_POINT('Ctrl Pts',(16.8253843166286,18.29509870991,11.0539319165923));
#187246=CARTESIAN_POINT('Ctrl Pts',(16.804008024655,18.3396440408911,11.0569148195271));
#187247=CARTESIAN_POINT('Ctrl Pts',(16.7842163233974,18.3848874840303,11.0598977224619));
#187248=CARTESIAN_POINT('Ctrl Pts',(16.7660496141036,18.4307050053664,11.0628806253966));
#187249=CARTESIAN_POINT('Ctrl Pts',(16.7358636223545,18.506835871923,11.0678370477141));
#187250=CARTESIAN_POINT('Ctrl Pts',(16.7100671742208,18.5848010792819,11.0727934700315));
#187251=CARTESIAN_POINT('Ctrl Pts',(16.6888585600977,18.6641129085501,11.077749892349));
#187252=CARTESIAN_POINT('Ctrl Pts',(16.6677318984798,18.7431182678595,11.082687162485));
#187253=CARTESIAN_POINT('Ctrl Pts',(16.6511578246458,18.8234596442757,11.087624432621));
#187254=CARTESIAN_POINT('Ctrl Pts',(16.639285644145,18.9046329531839,11.092561702757));
#187255=CARTESIAN_POINT('Ctrl Pts',(16.6274900435731,18.9852826644061,11.0974671256854));
#187256=CARTESIAN_POINT('Ctrl Pts',(16.6203359927514,19.0667533747576,11.1023725486138));
#187257=CARTESIAN_POINT('Ctrl Pts',(16.6179218376292,19.148532322459,11.1072779715423));
#187258=CARTESIAN_POINT('Ctrl Pts',(16.6173204835913,19.1689030517308,11.1084998880042));
#187259=CARTESIAN_POINT('Ctrl Pts',(16.6170129926863,19.1892928268081,11.1097218044662));
#187260=CARTESIAN_POINT('Ctrl Pts',(16.6170004031077,19.2096935705332,11.1109437209282));
#187261=CARTESIAN_POINT('',(16.6170004031077,19.2123064294672,10.8890562790718));
#187262=CARTESIAN_POINT('Ctrl Pts',(16.74541937607,19.9371102548029,10.1325348912934));
#187263=CARTESIAN_POINT('Ctrl Pts',(16.7957300871112,20.0748949844512,10.1420538203509));
#187264=CARTESIAN_POINT('Ctrl Pts',(16.8602294130613,20.2070927770557,10.1518904231319));
#187265=CARTESIAN_POINT('Ctrl Pts',(16.9705620701912,20.3839384574977,10.1654299263584));
#187266=CARTESIAN_POINT('Ctrl Pts',(17.005507726352,20.4348520887237,10.1693725855517));
#187267=CARTESIAN_POINT('Ctrl Pts',(17.0481243237945,20.4914669517243,10.1737463497107));
#187268=CARTESIAN_POINT('Ctrl Pts',(17.0536641593785,20.4987281854847,10.1743070950182));
#187269=CARTESIAN_POINT('Ctrl Pts',(17.0620088147972,20.5095202363625,10.1751398905875));
#187270=CARTESIAN_POINT('Ctrl Pts',(17.0647781206029,20.5130782026633,10.1754143490037));
#187271=CARTESIAN_POINT('Ctrl Pts',(17.0697578835671,20.5194341374356,10.1759044173227));
#187272=CARTESIAN_POINT('Ctrl Pts',(17.071964054018,20.5222353827532,10.1761203241256));
#187273=CARTESIAN_POINT('Ctrl Pts',(17.0767598421284,20.5282931980694,10.1765870517956));
#187274=CARTESIAN_POINT('Ctrl Pts',(17.0793519774033,20.5315477017296,10.1768376885868));
#187275=CARTESIAN_POINT('Ctrl Pts',(17.0866262033125,20.5406256645147,10.1775365670396));
#187276=CARTESIAN_POINT('Ctrl Pts',(17.0913296091945,20.5464320741603,10.1779833076267));
#187277=CARTESIAN_POINT('Ctrl Pts',(17.118952348447,20.5801659161903,10.1805779717675));
#187278=CARTESIAN_POINT('Ctrl Pts',(17.1425543053568,20.6075296900622,10.1826795136911));
#187279=CARTESIAN_POINT('Ctrl Pts',(17.220974678788,20.6938773863978,10.1893509065886));
#187280=CARTESIAN_POINT('Ctrl Pts',(17.2784630051519,20.7503456564029,10.1937780097012));
#187281=CARTESIAN_POINT('Ctrl Pts',(17.4407097909254,20.8924759219074,10.2055350900232));
#187282=CARTESIAN_POINT('Ctrl Pts',(17.5506782810402,20.9715989992329,10.2127865849435));
#187283=CARTESIAN_POINT('Ctrl Pts',(17.721908541426,21.071466675794,10.2239369567949));
#187284=CARTESIAN_POINT('Ctrl Pts',(17.7777672529595,21.100783903157,10.2275505940441));
#187285=CARTESIAN_POINT('Ctrl Pts',(17.8461537344153,21.1328673151038,10.2319867423496));
#187286=CARTESIAN_POINT('Ctrl Pts',(17.8575065567011,21.1380714055328,10.232723519243));
#187287=CARTESIAN_POINT('Ctrl Pts',(17.876211673527,21.14644627516,10.2339382844348));
#187288=CARTESIAN_POINT('Ctrl Pts',(17.8835371877504,21.1496763781902,10.2344142333636));
#187289=CARTESIAN_POINT('Ctrl Pts',(17.8967322475627,21.1554054117174,10.2352719829291));
#187290=CARTESIAN_POINT('Ctrl Pts',(17.9025951264354,21.1579195230476,10.2356532592963));
#187291=CARTESIAN_POINT('Ctrl Pts',(17.9150972022701,21.1632138755813,10.2364666731196));
#187292=CARTESIAN_POINT('Ctrl Pts',(17.9217393813976,21.1659868269677,10.2368990527367));
#187293=CARTESIAN_POINT('Ctrl Pts',(17.9396436270696,21.1733544269303,10.238065215204));
#187294=CARTESIAN_POINT('Ctrl Pts',(17.9509312371049,21.1778859262824,10.2388011221852));
#187295=CARTESIAN_POINT('Ctrl Pts',(18.0072714593683,21.1999423001178,10.2424782716742));
#187296=CARTESIAN_POINT('Ctrl Pts',(18.0528730329247,21.2160165336841,10.2454676607904));
#187297=CARTESIAN_POINT('Ctrl Pts',(18.1854403586944,21.2577011130997,10.2542017476429));
#187298=CARTESIAN_POINT('Ctrl Pts',(18.2735461230385,21.2793041892006,10.2600638156925));
#187299=CARTESIAN_POINT('Ctrl Pts',(18.5213290176749,21.3234400849024,10.2765863247773));
#187300=CARTESIAN_POINT('Ctrl Pts',(18.682610212615,21.3334973897724,10.2874126602705));
#187301=CARTESIAN_POINT('Ctrl Pts',(18.8634556716809,21.3241328638617,10.2987727045214));
#187302=CARTESIAN_POINT('Ctrl Pts',(18.8834208643317,21.322815035384,10.3000154249877));
#187303=CARTESIAN_POINT('Ctrl Pts',(18.909726645604,21.3207037410137,10.301635117501));
#187304=CARTESIAN_POINT('Ctrl Pts',(18.9160858563881,21.3201644014005,10.3020252983786));
#187305=CARTESIAN_POINT('Ctrl Pts',(18.9263462544684,21.3192474424093,10.3026525304847));
#187306=CARTESIAN_POINT('Ctrl Pts',(18.9302489451616,21.3188877370806,10.3028905666247));
#187307=CARTESIAN_POINT('Ctrl Pts',(18.9377547927568,21.318174907649,10.3033472996069));
#187308=CARTESIAN_POINT('Ctrl Pts',(18.9413580460358,21.3178233784252,10.3035660803881));
#187309=CARTESIAN_POINT('Ctrl Pts',(18.9498803941602,21.3169698726508,10.3040824357027));
#187310=CARTESIAN_POINT('Ctrl Pts',(18.9547987005138,21.316459898473,10.3043795612766));
#187311=CARTESIAN_POINT('Ctrl Pts',(18.9711071481925,21.3147111180669,10.3053620474774));
#187312=CARTESIAN_POINT('Ctrl Pts',(18.98248924533,21.3133970548121,10.3060433101046));
#187313=CARTESIAN_POINT('Ctrl Pts',(19.0903407899513,21.3000574687938,10.3124612282572));
#187314=CARTESIAN_POINT('Ctrl Pts',(19.1858975522566,21.2814910665904,10.3178657671543));
#187315=CARTESIAN_POINT('Ctrl Pts',(19.3524153639701,21.2370533582304,10.3272974760259));
#187316=CARTESIAN_POINT('Ctrl Pts',(19.4238995390087,21.2138401417208,10.3313511972611));
#187317=CARTESIAN_POINT('Ctrl Pts',(19.6179294553143,21.1392086601816,10.3426813823989));
#187318=CARTESIAN_POINT('Ctrl Pts',(19.7370824942925,21.0799940189519,10.3500352953538));
#187319=CARTESIAN_POINT('Ctrl Pts',(19.8633132958297,21.0016953116394,10.3587362688878));
#187320=CARTESIAN_POINT('Ctrl Pts',(19.8766349620666,20.9932243244337,10.3596662979032));
#187321=CARTESIAN_POINT('Ctrl Pts',(19.8966275950702,20.9801951051994,10.3610805368106));
#187322=CARTESIAN_POINT('Ctrl Pts',(19.9033694413513,20.9757462571005,10.3615606658));
#187323=CARTESIAN_POINT('Ctrl Pts',(19.9153957552,20.9677110903517,10.3624230058577));
#187324=CARTESIAN_POINT('Ctrl Pts',(19.9206897917394,20.9641392192776,10.3628046691847));
#187325=CARTESIAN_POINT('Ctrl Pts',(19.9318793905945,20.9565157227513,10.3636157769336));
#187326=CARTESIAN_POINT('Ctrl Pts',(19.9377707299438,20.952458067413,10.3640454474057));
#187327=CARTESIAN_POINT('Ctrl Pts',(19.9534592811113,20.9415349406939,10.3651967460016));
#187328=CARTESIAN_POINT('Ctrl Pts',(19.9632189454135,20.9346162259274,10.3659204056326));
#187329=CARTESIAN_POINT('Ctrl Pts',(20.0101715068826,20.9007295216238,10.3694385686195));
#187330=CARTESIAN_POINT('Ctrl Pts',(20.0465361870195,20.8726400974848,10.3722763496522));
#187331=CARTESIAN_POINT('Ctrl Pts',(20.2126103330943,20.7355034668146,10.3857885327702));
#187332=CARTESIAN_POINT('Ctrl Pts',(20.3298229084178,20.6123319588386,10.3970390207031));
#187333=CARTESIAN_POINT('Ctrl Pts',(20.4905160495344,20.396843266539,10.4147482674157));
#187334=CARTESIAN_POINT('Ctrl Pts',(20.5442674237925,20.3130478363557,10.4212274626824));
#187335=CARTESIAN_POINT('Ctrl Pts',(20.5965812906995,20.217267320545,10.4279703788607));
#187336=CARTESIAN_POINT('Ctrl Pts',(20.6011699521907,20.2087270983095,10.4285660453203));
#187337=CARTESIAN_POINT('Ctrl Pts',(20.6078582813773,20.1960713072625,10.4294402446069));
#187338=CARTESIAN_POINT('Ctrl Pts',(20.6100033294292,20.1919800446404,10.42972154322));
#187339=CARTESIAN_POINT('Ctrl Pts',(20.6137849628936,20.1847095452751,10.4302190766529));
#187340=CARTESIAN_POINT('Ctrl Pts',(20.6154269008567,20.1815331538352,10.4304356463494));
#187341=CARTESIAN_POINT('Ctrl Pts',(20.6189274717902,20.1747188977478,10.4308985353165));
#187342=CARTESIAN_POINT('Ctrl Pts',(20.6207836201712,20.1710798191236,10.4311446983954));
#187343=CARTESIAN_POINT('Ctrl Pts',(20.6258495529179,20.1610763529531,10.43181859432));
#187344=CARTESIAN_POINT('Ctrl Pts',(20.6290377800182,20.1547010241123,10.4322449951897));
#187345=CARTESIAN_POINT('Ctrl Pts',(20.6458835129206,20.1205858658636,10.4345109559536));
#187346=CARTESIAN_POINT('Ctrl Pts',(20.6589650341288,20.0925638710295,10.4363167906306));
#187347=CARTESIAN_POINT('Ctrl Pts',(20.6966949899269,20.0068938756825,10.441701271943));
#187348=CARTESIAN_POINT('Ctrl Pts',(20.7194025216674,19.9484256980049,10.4451932067317));
#187349=CARTESIAN_POINT('Ctrl Pts',(20.7825323192419,19.7617003962861,10.4560260400965));
#187350=CARTESIAN_POINT('Ctrl Pts',(20.8133570332004,19.6305600322206,10.4631939275482));
#187351=CARTESIAN_POINT('Ctrl Pts',(20.8370589769717,19.4569598758478,10.4729176038633));
#187352=CARTESIAN_POINT('Ctrl Pts',(20.8414079545718,19.4163893589733,10.4752044795843));
#187353=CARTESIAN_POINT('Ctrl Pts',(20.8483658788832,19.3272364043524,10.480286725375));
#187354=CARTESIAN_POINT('Ctrl Pts',(20.8504777991199,19.2786399537743,10.4830939607998));
#187355=CARTESIAN_POINT('Ctrl Pts',(20.8510278249307,19.2174109296055,10.4866951579177));
#187356=CARTESIAN_POINT('Ctrl Pts',(20.8510284650092,19.204804876958,10.4874399796913));
#187357=CARTESIAN_POINT('Ctrl Pts',(20.8508510753374,19.1848306978137,10.4886258058009));
#187358=CARTESIAN_POINT('Ctrl Pts',(20.8507471539886,19.1774620884726,10.4890644859234));
#187359=CARTESIAN_POINT('Ctrl Pts',(20.8504818440078,19.1637340363762,10.4898841002203));
#187360=CARTESIAN_POINT('Ctrl Pts',(20.8503302598147,19.1573744710327,10.4902647225078));
#187361=CARTESIAN_POINT('Ctrl Pts',(20.8499299453271,19.1432520080514,10.4911120704385));
#187362=CARTESIAN_POINT('Ctrl Pts',(20.8496671537285,19.1354896293758,10.4915792320877));
#187363=CARTESIAN_POINT('Ctrl Pts',(20.8487795583968,19.1129417549045,10.4929404348042));
#187364=CARTESIAN_POINT('Ctrl Pts',(20.8480424372916,19.0981613721878,10.4938379817583));
#187365=CARTESIAN_POINT('Ctrl Pts',(20.8409614218368,18.9809035027416,10.501001623834));
#187366=CARTESIAN_POINT('Ctrl Pts',(20.8273259251446,18.8790180880072,10.5074978158596));
#187367=CARTESIAN_POINT('Ctrl Pts',(20.7748106556447,18.6273664013535,10.5241841356418));
#187368=CARTESIAN_POINT('Ctrl Pts',(20.7268215378695,18.4801136197315,10.534558879243));
#187369=CARTESIAN_POINT('Ctrl Pts',(20.641028217822,18.2902151943768,10.5480316975662));
#187370=CARTESIAN_POINT('Ctrl Pts',(20.6169351578503,18.2418985904145,10.5514635448109));
#187371=CARTESIAN_POINT('Ctrl Pts',(20.5868215894256,18.1868820362228,10.5553326854529));
#187372=CARTESIAN_POINT('Ctrl Pts',(20.5825760385602,18.1792383600413,10.5558693418908));
#187373=CARTESIAN_POINT('Ctrl Pts',(20.5760796170467,18.1677110523727,10.5566770447229));
#187374=CARTESIAN_POINT('Ctrl Pts',(20.5738636116541,18.1638080237369,10.5569502415293));
#187375=CARTESIAN_POINT('Ctrl Pts',(20.5698655446414,18.1568181343681,10.557438956443));
#187376=CARTESIAN_POINT('Ctrl Pts',(20.5680880925522,18.1537287135389,10.5576547644159));
#187377=CARTESIAN_POINT('Ctrl Pts',(20.5642111785997,18.1470293800548,10.5581223073707));
#187378=CARTESIAN_POINT('Ctrl Pts',(20.5621088423131,18.1434211974162,10.5583738527293));
#187379=CARTESIAN_POINT('Ctrl Pts',(20.556179320107,18.1333133958066,10.5590778357925));
#187380=CARTESIAN_POINT('Ctrl Pts',(20.5523280104854,18.1268279003548,10.5595287367539));
#187381=CARTESIAN_POINT('Ctrl Pts',(20.5292167185712,18.0883787182219,10.5621979881362));
#187382=CARTESIAN_POINT('Ctrl Pts',(20.5091476846135,18.05690611673,10.5643667870077));
#187383=CARTESIAN_POINT('Ctrl Pts',(20.4406577061334,17.9555164513515,10.5713561834721));
#187384=CARTESIAN_POINT('Ctrl Pts',(20.388853691367,17.8879803445313,10.5760179379409));
#187385=CARTESIAN_POINT('Ctrl Pts',(20.2162719043821,17.6890418045363,10.5903546240858));
#187386=CARTESIAN_POINT('Ctrl Pts',(20.0828856112584,17.5696628006295,10.5999274915264));
#187387=CARTESIAN_POINT('Ctrl Pts',(19.917373904607,17.4554847428305,10.611614148404));
#187388=CARTESIAN_POINT('Ctrl Pts',(19.8984215783637,17.4428569218332,10.6129485197993));
#187389=CARTESIAN_POINT('Ctrl Pts',(19.8712712802945,17.4253926856173,10.6148564091392));
#187390=CARTESIAN_POINT('Ctrl Pts',(19.8632383315085,17.4203017472716,10.6154204447334));
#187391=CARTESIAN_POINT('Ctrl Pts',(19.85011559208,17.4121085326836,10.6163412486508));
#187392=CARTESIAN_POINT('Ctrl Pts',(19.8450464652129,17.4089732862449,10.6166967945617));
#187393=CARTESIAN_POINT('Ctrl Pts',(19.8343958162144,17.4024479013006,10.6174435507512));
#187394=CARTESIAN_POINT('Ctrl Pts',(19.8288117202931,17.3990621032503,10.617834915302));
#187395=CARTESIAN_POINT('Ctrl Pts',(19.8154676484916,17.391055414418,10.6187698147042));
#187396=CARTESIAN_POINT('Ctrl Pts',(19.807693639502,17.3864582674368,10.6193142079375));
#187397=CARTESIAN_POINT('Ctrl Pts',(19.7812966117848,17.3710755587793,10.6211619885186));
#187398=CARTESIAN_POINT('Ctrl Pts',(19.762539099839,17.3605245451789,10.622473796705));
#187399=CARTESIAN_POINT('Ctrl Pts',(19.5850852396242,17.2642392365245,10.6348767858291));
#187400=CARTESIAN_POINT('Ctrl Pts',(19.416230969203,17.1988472306411,10.6467203448037));
#187401=CARTESIAN_POINT('Ctrl Pts',(19.1251260688293,17.1270139337721,10.6665283006269));
#187402=CARTESIAN_POINT('Ctrl Pts',(19.0068414311021,17.1082537691679,10.6743928266103));
#187403=CARTESIAN_POINT('Ctrl Pts',(18.8781140149752,17.0988895626419,10.6823645329544));
#187404=CARTESIAN_POINT('Ctrl Pts',(18.8686291192085,17.0982637748847,10.6829484216145));
#187405=CARTESIAN_POINT('Ctrl Pts',(18.8545656802276,17.0974310004847,10.6838086845926));
#187406=CARTESIAN_POINT('Ctrl Pts',(18.8499903137156,17.0971749724736,10.6840877015579));
#187407=CARTESIAN_POINT('Ctrl Pts',(18.8418471005566,17.0967458143016,10.6845827226335));
#187408=CARTESIAN_POINT('Ctrl Pts',(18.8382796185922,17.096566855953,10.6847990489774));
#187409=CARTESIAN_POINT('Ctrl Pts',(18.8306073468514,17.0962014507775,10.6852631163605));
#187410=CARTESIAN_POINT('Ctrl Pts',(18.8265024742595,17.0960179253301,10.6855106922892));
#187411=CARTESIAN_POINT('Ctrl Pts',(18.8151671424244,17.0955441961839,10.6861924529052));
#187412=CARTESIAN_POINT('Ctrl Pts',(18.8079356111265,17.0952791082577,10.6866252533551));
#187413=CARTESIAN_POINT('Ctrl Pts',(18.7682606336491,17.0940284023046,10.6889887285462));
#187414=CARTESIAN_POINT('Ctrl Pts',(18.7357972673219,17.0937518882932,10.6908821457287));
#187415=CARTESIAN_POINT('Ctrl Pts',(18.5406086071179,17.0965791991765,10.7020913157596));
#187416=CARTESIAN_POINT('Ctrl Pts',(18.3786765670616,17.1176933614959,10.7106933723548));
#187417=CARTESIAN_POINT('Ctrl Pts',(18.107397307336,17.1854854424246,10.7260011154506));
#187418=CARTESIAN_POINT('Ctrl Pts',(17.9965994894125,17.2231430171881,10.7325235546343));
#187419=CARTESIAN_POINT('Ctrl Pts',(17.8763668409597,17.2754486820515,10.7402047325094));
#187420=CARTESIAN_POINT('Ctrl Pts',(17.8633107589045,17.2812866092623,10.7410469283496));
#187421=CARTESIAN_POINT('Ctrl Pts',(17.8426290491511,17.2907868951309,10.7423944032879));
#187422=CARTESIAN_POINT('Ctrl Pts',(17.8349643491886,17.294363509809,10.7428967349929));
#187423=CARTESIAN_POINT('Ctrl Pts',(17.8214861888465,17.3007515233942,10.7437853816656));
#187424=CARTESIAN_POINT('Ctrl Pts',(17.8156637403704,17.3035437853665,10.7441710294786));
#187425=CARTESIAN_POINT('Ctrl Pts',(17.8097007059104,17.3064370989501,10.7445678198506));
#187426=CARTESIAN_POINT('Ctrl Pts',(17.8095472134244,17.306511597698,10.7445780347475));
#187427=CARTESIAN_POINT('Ctrl Pts',(17.8092663778586,17.3066479453308,10.7445967265874));
#187428=CARTESIAN_POINT('Ctrl Pts',(17.8091390319691,17.306709788437,10.7446052033284));
#187429=CARTESIAN_POINT('Ctrl Pts',(17.8089024434121,17.3068247124945,10.7446209533723));
#187430=CARTESIAN_POINT('Ctrl Pts',(17.8087931994503,17.3068777899074,10.7446282265344));
#187431=CARTESIAN_POINT('Ctrl Pts',(17.8085902492665,17.3069764171358,10.7446417395748));
#187432=CARTESIAN_POINT('Ctrl Pts',(17.808496541362,17.3070219647001,10.7446479793979));
#187433=CARTESIAN_POINT('Ctrl Pts',(17.8083224568012,17.3071065959447,10.7446595722084));
#187434=CARTESIAN_POINT('Ctrl Pts',(17.8082420785269,17.3071456781525,10.7446649251805));
#187435=CARTESIAN_POINT('Ctrl Pts',(17.8080927577167,17.307218293878,10.744674870173));
#187436=CARTESIAN_POINT('Ctrl Pts',(17.8080238136811,17.3072518264625,10.7446794622027));
#187437=CARTESIAN_POINT('Ctrl Pts',(17.8078957346041,17.3073141293953,10.7446879934013));
#187438=CARTESIAN_POINT('Ctrl Pts',(17.8078365979246,17.3073428993172,10.7446919326125));
#187439=CARTESIAN_POINT('Ctrl Pts',(17.8077088154405,17.307405072702,10.744700444858));
#187440=CARTESIAN_POINT('Ctrl Pts',(17.8076401687993,17.3074384777564,10.7447050180124));
#187441=CARTESIAN_POINT('Ctrl Pts',(17.8075052320939,17.3075041501287,10.7447140078214));
#187442=CARTESIAN_POINT('Ctrl Pts',(17.8074389445209,17.3075364159238,10.7447184242929));
#187443=CARTESIAN_POINT('Ctrl Pts',(17.8073086442183,17.3075998486424,10.7447271061314));
#187444=CARTESIAN_POINT('Ctrl Pts',(17.8072446309937,17.3076310155184,10.7447313715156));
#187445=CARTESIAN_POINT('Ctrl Pts',(17.807118796977,17.3076922896677,10.7447397566241));
#187446=CARTESIAN_POINT('Ctrl Pts',(17.8070569756069,17.3077223969539,10.7447438763723));
#187447=CARTESIAN_POINT('Ctrl Pts',(17.8069354460599,17.3077815897174,10.744751975446));
#187448=CARTESIAN_POINT('Ctrl Pts',(17.8068757371987,17.307810675278,10.7447559548034));
#187449=CARTESIAN_POINT('Ctrl Pts',(17.8067583561941,17.3078678611018,10.7447637781518));
#187450=CARTESIAN_POINT('Ctrl Pts',(17.8067006834021,17.3078959614482,10.7447676221733));
#187451=CARTESIAN_POINT('Ctrl Pts',(17.8065873010777,17.307951211945,10.7447751797086));
#187452=CARTESIAN_POINT('Ctrl Pts',(17.8065315908239,17.3079783622302,10.7447788932586));
#187453=CARTESIAN_POINT('Ctrl Pts',(17.806422063013,17.3080317463502,10.7447861945193));
#187454=CARTESIAN_POINT('Ctrl Pts',(17.8063682446217,17.30805798039,10.7447897822746));
#187455=CARTESIAN_POINT('Ctrl Pts',(17.8062624323477,17.3081095646591,10.744796836459));
#187456=CARTESIAN_POINT('Ctrl Pts',(17.8062104376947,17.3081349150761,10.7448003029293));
#187457=CARTESIAN_POINT('Ctrl Pts',(17.806108207636,17.3081847633608,10.7448071188641));
#187458=CARTESIAN_POINT('Ctrl Pts',(17.8060579713042,17.308209261505,10.7448104683809));
#187459=CARTESIAN_POINT('Ctrl Pts',(17.8059591948887,17.3082574354464,10.7448170545809));
#187460=CARTESIAN_POINT('Ctrl Pts',(17.8059106538732,17.308281111535,10.7448202913175));
#187461=CARTESIAN_POINT('Ctrl Pts',(17.8058152075798,17.3083276703955,10.7448266559656));
#187462=CARTESIAN_POINT('Ctrl Pts',(17.8057683012866,17.3083505535107,10.7448297839365));
#187463=CARTESIAN_POINT('Ctrl Pts',(17.80567606627,17.3083955543501,10.7448359349077));
#187464=CARTESIAN_POINT('Ctrl Pts',(17.8056307364209,17.3084176724819,10.7448389579754));
#187465=CARTESIAN_POINT('Ctrl Pts',(17.8055416032693,17.30846116783,10.7448449025198));
#187466=CARTESIAN_POINT('Ctrl Pts',(17.8054977987418,17.3084825455108,10.7448478240708));
#187467=CARTESIAN_POINT('Ctrl Pts',(17.8054116380863,17.3085245977047,10.7448535707732));
#187468=CARTESIAN_POINT('Ctrl Pts',(17.8053692955266,17.3085452654717,10.7448563950126));
#187469=CARTESIAN_POINT('Ctrl Pts',(17.8052860248987,17.3085859140224,10.7448619493331));
#187470=CARTESIAN_POINT('Ctrl Pts',(17.8052450968604,17.3086058946768,10.7448646794059));
#187471=CARTESIAN_POINT('Ctrl Pts',(17.805164605607,17.3086451929093,10.7448700486875));
#187472=CARTESIAN_POINT('Ctrl Pts',(17.8051250422739,17.3086645104378,10.7448726878984));
#187473=CARTESIAN_POINT('Ctrl Pts',(17.7985011501907,17.311899004069,10.7453145718262));
#187474=CARTESIAN_POINT('Ctrl Pts',(17.7919336235539,17.3151483098601,10.7457550069991));
#187475=CARTESIAN_POINT('Ctrl Pts',(17.7737986951425,17.3242381258899,10.7469776667063));
#187476=CARTESIAN_POINT('Ctrl Pts',(17.7622679932774,17.3301507740256,10.747762415341));
#187477=CARTESIAN_POINT('Ctrl Pts',(17.7366952585574,17.3435617439011,10.7495195293927));
#187478=CARTESIAN_POINT('Ctrl Pts',(17.7226821651151,17.3511132822686,10.7504937426596));
#187479=CARTESIAN_POINT('Ctrl Pts',(17.6796445474024,17.3749360815964,10.7535215780836));
#187480=CARTESIAN_POINT('Ctrl Pts',(17.6509185467627,17.3917335253399,10.7555935546413));
#187481=CARTESIAN_POINT('Ctrl Pts',(17.5398316012297,17.4602549366746,10.7638101234837));
#187482=CARTESIAN_POINT('Ctrl Pts',(17.460686968916,17.5169466884081,10.7701220025741));
#187483=CARTESIAN_POINT('Ctrl Pts',(17.2630943013048,17.6801745733501,10.7869860853912));
#187484=CARTESIAN_POINT('Ctrl Pts',(17.1522643756485,17.7949814291251,10.7976554552696));
#187485=CARTESIAN_POINT('Ctrl Pts',(17.0465207438521,17.9325978306237,10.8084633883669));
#187486=CARTESIAN_POINT('Ctrl Pts',(17.0378225548171,17.9441612386155,10.8093575252665));
#187487=CARTESIAN_POINT('Ctrl Pts',(17.0259221726123,17.9603239779325,10.8105869635517));
#187488=CARTESIAN_POINT('Ctrl Pts',(17.0226188805738,17.9648479056299,10.8109289005769));
#187489=CARTESIAN_POINT('Ctrl Pts',(17.0173544802148,17.972118025886,10.811474849864));
#187490=CARTESIAN_POINT('Ctrl Pts',(17.0153819412441,17.9748558519041,10.8116796437401));
#187491=CARTESIAN_POINT('Ctrl Pts',(17.0112833764433,17.980573312696,10.8121056275169));
#187492=CARTESIAN_POINT('Ctrl Pts',(17.0091585262205,17.9835537533395,10.8123267317868));
#187493=CARTESIAN_POINT('Ctrl Pts',(17.0040506283553,17.9907578482032,10.8128589034139));
#187494=CARTESIAN_POINT('Ctrl Pts',(17.00107527965,17.9949869851174,10.8131694435653));
#187495=CARTESIAN_POINT('Ctrl Pts',(16.9907892868477,18.009721837901,10.8142450855552));
#187496=CARTESIAN_POINT('Ctrl Pts',(16.9835582754486,18.0202831569854,10.8150049481536));
#187497=CARTESIAN_POINT('Ctrl Pts',(16.9419209234204,18.0822960722414,10.8194062547253));
#187498=CARTESIAN_POINT('Ctrl Pts',(16.909685385747,18.1351758513538,10.8229192027546));
#187499=CARTESIAN_POINT('Ctrl Pts',(16.7964878859874,18.3406270456282,10.8359751612939));
#187500=CARTESIAN_POINT('Ctrl Pts',(16.7319777455018,18.5014830941564,10.8450643141511));
#187501=CARTESIAN_POINT('Ctrl Pts',(16.6773854536263,18.7073623694484,10.8569814755598));
#187502=CARTESIAN_POINT('Ctrl Pts',(16.6681681803629,18.7466155845529,10.8592625159251));
#187503=CARTESIAN_POINT('Ctrl Pts',(16.65885732692,18.7920622410054,10.8619252933743));
#187504=CARTESIAN_POINT('Ctrl Pts',(16.6576628198152,18.7980231571865,10.8622749747557));
#187505=CARTESIAN_POINT('Ctrl Pts',(16.6558534174598,18.8072588906171,10.8628174652843));
#187506=CARTESIAN_POINT('Ctrl Pts',(16.6552205441102,18.8105301815036,10.8630097508983));
#187507=CARTESIAN_POINT('Ctrl Pts',(16.6491723848835,18.8421934826621,10.8648722695303));
#187508=CARTESIAN_POINT('Ctrl Pts',(16.6443315775463,18.8706910269824,10.8665591920273));
#187509=CARTESIAN_POINT('Ctrl Pts',(16.6385322992379,18.909646377655,10.8688831261859));
#187510=CARTESIAN_POINT('Ctrl Pts',(16.6370657829911,18.9200261623686,10.8695040672793));
#187511=CARTESIAN_POINT('Ctrl Pts',(16.634862066262,18.9365064863082,10.8704928394284));
#187512=CARTESIAN_POINT('Ctrl Pts',(16.6340742197246,18.9426001676087,10.8708590665784));
#187513=CARTESIAN_POINT('Ctrl Pts',(16.6325483600515,18.9548202163897,10.8715947703817));
#187514=CARTESIAN_POINT('Ctrl Pts',(16.6318105821765,18.9609465518859,10.8719642506085));
#187515=CARTESIAN_POINT('Ctrl Pts',(16.6303836082957,18.9732486772884,10.8727075230525));
#187516=CARTESIAN_POINT('Ctrl Pts',(16.6296947992168,18.9794244495415,10.873081323587));
#187517=CARTESIAN_POINT('Ctrl Pts',(16.6281826817362,18.9935460159799,10.873937626837));
#187518=CARTESIAN_POINT('Ctrl Pts',(16.6273771408042,19.0014935813907,10.8744206846731));
#187519=CARTESIAN_POINT('Ctrl Pts',(16.6254321893437,19.0218293069931,10.8756596709703));
#187520=CARTESIAN_POINT('Ctrl Pts',(16.6243569721749,19.0342231689276,10.8764176018163));
#187521=CARTESIAN_POINT('Ctrl Pts',(16.6190952486465,19.1017850249937,10.8805650384811));
#187522=CARTESIAN_POINT('Ctrl Pts',(16.6169637967665,19.1570864436259,10.8840179272398));
#187523=CARTESIAN_POINT('Ctrl Pts',(16.6170004651127,19.2124033128222,10.8875305623383));
#187524=CARTESIAN_POINT('Ctrl Pts',(16.7454193623258,19.9371102171621,10.9336112429045));
#187525=CARTESIAN_POINT('Ctrl Pts',(16.7173390128125,19.8602072373921,10.9286590653809));
#187526=CARTESIAN_POINT('Ctrl Pts',(16.6936915503228,19.781585811724,10.9237068878573));
#187527=CARTESIAN_POINT('Ctrl Pts',(16.6746638706561,19.7017379202578,10.9187547103338));
#187528=CARTESIAN_POINT('Ctrl Pts',(16.6556455622465,19.6219293544019,10.9138049717901));
#187529=CARTESIAN_POINT('Ctrl Pts',(16.6412426570166,19.5408957414284,10.9088552332465));
#187530=CARTESIAN_POINT('Ctrl Pts',(16.6315940722725,19.4591497835104,10.9039054947028));
#187531=CARTESIAN_POINT('Ctrl Pts',(16.6219454875284,19.3774038255923,10.8989557561591));
#187532=CARTESIAN_POINT('Ctrl Pts',(16.6170514009658,19.2949457511214,10.8940060176155));
#187533=CARTESIAN_POINT('Ctrl Pts',(16.6170004031077,19.2123064294672,10.8890562790718));
#187534=CARTESIAN_POINT('Origin',(18.734,19.211,0.));
#187535=CARTESIAN_POINT('',(16.7454193623241,19.9371102171575,11.9535387334123));
#187536=CARTESIAN_POINT('',(16.7460270442576,19.936878801227,11.7337477294316));
#187537=CARTESIAN_POINT('',(16.7454193623258,19.9371102171621,0.));
#187538=CARTESIAN_POINT('Ctrl Pts',(16.7454193623241,19.9371102171575,11.9535387334123));
#187539=CARTESIAN_POINT('Ctrl Pts',(16.7451290268508,19.9363150823599,11.9534866359792));
#187540=CARTESIAN_POINT('Ctrl Pts',(16.7448391668873,19.9355197696119,11.9534345643187));
#187541=CARTESIAN_POINT('Ctrl Pts',(16.7420974952995,19.9279831713629,11.9529414752215));
#187542=CARTESIAN_POINT('Ctrl Pts',(16.7396794458117,19.921229531058,11.9525023096659));
#187543=CARTESIAN_POINT('Ctrl Pts',(16.7359349682283,19.9106012424581,11.951815566168));
#187544=CARTESIAN_POINT('Ctrl Pts',(16.7345854012506,19.9067348867221,11.9515666491811));
#187545=CARTESIAN_POINT('Ctrl Pts',(16.7320789914907,19.8994867825225,11.9511017428328));
#187546=CARTESIAN_POINT('Ctrl Pts',(16.7309195068312,19.8961060590327,11.9508856034616));
#187547=CARTESIAN_POINT('Ctrl Pts',(16.7282860711328,19.8883638826122,11.9503922206569));
#187548=CARTESIAN_POINT('Ctrl Pts',(16.7268177842271,19.8840005553657,11.9501153139117));
#187549=CARTESIAN_POINT('Ctrl Pts',(16.722327343384,19.8705108381309,11.9492626834733));
#187550=CARTESIAN_POINT('Ctrl Pts',(16.7193530648855,19.8613684784025,11.9486897092102));
#187551=CARTESIAN_POINT('Ctrl Pts',(16.6905473891357,19.7707312275937,11.9430544686176));
#187552=CARTESIAN_POINT('Ctrl Pts',(16.6696094506914,19.6877523770249,11.9382547439852));
#187553=CARTESIAN_POINT('Ctrl Pts',(16.6294008130744,19.474768539116,11.9263203647501));
#187554=CARTESIAN_POINT('Ctrl Pts',(16.6170990834764,19.3438276878587,11.9193213153926));
#187555=CARTESIAN_POINT('Ctrl Pts',(16.616931378433,19.1203529379548,11.9069620233889));
#187556=CARTESIAN_POINT('Ctrl Pts',(16.6228899847845,19.0282216733242,11.9017508201384));
#187557=CARTESIAN_POINT('Ctrl Pts',(16.6366195088672,18.9231219351655,11.8955371625626));
#187558=CARTESIAN_POINT('Ctrl Pts',(16.6385368144155,18.9094826219187,11.894725665816));
#187559=CARTESIAN_POINT('Ctrl Pts',(16.6418231765306,18.8876517422287,11.893418186782));
#187560=CARTESIAN_POINT('Ctrl Pts',(16.6431076013345,18.8794476954235,11.8929248814234));
#187561=CARTESIAN_POINT('Ctrl Pts',(16.6454726643803,18.864901816223,11.8920466899971));
#187562=CARTESIAN_POINT('Ctrl Pts',(16.6465340101855,18.8585569203376,11.8916624206906));
#187563=CARTESIAN_POINT('Ctrl Pts',(16.6488043608628,18.8453544977507,11.8908602872554));
#187564=CARTESIAN_POINT('Ctrl Pts',(16.650018311446,18.838497910394,11.8904422699565));
#187565=CARTESIAN_POINT('Ctrl Pts',(16.6532558832587,18.8207228839739,11.8893548175654));
#187566=CARTESIAN_POINT('Ctrl Pts',(16.6553316037841,18.8098142601474,11.8886837297044));
#187567=CARTESIAN_POINT('Ctrl Pts',(16.6646897663983,18.7626573631951,11.8857662552718));
#187568=CARTESIAN_POINT('Ctrl Pts',(16.6728349235718,18.7265887901512,11.8834924945459));
#187569=CARTESIAN_POINT('Ctrl Pts',(16.6969459261816,18.6314844021895,11.8773804480956));
#187570=CARTESIAN_POINT('Ctrl Pts',(16.7145314183952,18.5728987707211,11.8734934714816));
#187571=CARTESIAN_POINT('Ctrl Pts',(16.786380717627,18.3664523620685,11.8593774937429));
#187572=CARTESIAN_POINT('Ctrl Pts',(16.8545581904161,18.2239974661177,11.8488054422961));
#187573=CARTESIAN_POINT('Ctrl Pts',(16.9705615847297,18.0380622514951,11.8345700363483));
#187574=CARTESIAN_POINT('Ctrl Pts',(17.0055074497953,17.9871482818579,11.8306273509307));
#187575=CARTESIAN_POINT('Ctrl Pts',(17.0481242922943,17.9305330896517,11.8262535613372));
#187576=CARTESIAN_POINT('Ctrl Pts',(17.0536641360199,17.9232718448985,11.8256928151803));
#187577=CARTESIAN_POINT('Ctrl Pts',(17.0620088016684,17.912479780531,11.8248600185695));
#187578=CARTESIAN_POINT('Ctrl Pts',(17.0647781094392,17.908921811637,11.824585559953));
#187579=CARTESIAN_POINT('Ctrl Pts',(17.0697578748995,17.9025658735866,11.8240954913808));
#187580=CARTESIAN_POINT('Ctrl Pts',(17.0719640458661,17.8997646275772,11.8238795845244));
#187581=CARTESIAN_POINT('Ctrl Pts',(17.0767598339052,17.8937068122788,11.8234128568554));
#187582=CARTESIAN_POINT('Ctrl Pts',(17.0793519685854,17.8904523093223,11.823162220118));
#187583=CARTESIAN_POINT('Ctrl Pts',(17.0866261898216,17.8813743522364,11.822463342103));
#187584=CARTESIAN_POINT('Ctrl Pts',(17.0913295915774,17.8755679475459,11.8220166018962));
#187585=CARTESIAN_POINT('Ctrl Pts',(17.1189522482874,17.8418342052015,11.8194219454171));
#187586=CARTESIAN_POINT('Ctrl Pts',(17.1425541219988,17.8144705220699,11.8173204104481));
#187587=CARTESIAN_POINT('Ctrl Pts',(17.2209740847264,17.7281232449019,11.8106490502104));
#187588=CARTESIAN_POINT('Ctrl Pts',(17.2784620503688,17.6716552706437,11.8062219711733));
#187589=CARTESIAN_POINT('Ctrl Pts',(17.4407086333482,17.5295249399828,11.7944648949924));
#187590=CARTESIAN_POINT('Ctrl Pts',(17.5506773655383,17.4504015889066,11.7872133827168));
#187591=CARTESIAN_POINT('Ctrl Pts',(17.7219080787525,17.3505335687752,11.776062980708));
#187592=CARTESIAN_POINT('Ctrl Pts',(17.7777669708736,17.3212162325674,11.772449331803));
#187593=CARTESIAN_POINT('Ctrl Pts',(17.8461536571563,17.2891327204718,11.7680131702154));
#187594=CARTESIAN_POINT('Ctrl Pts',(17.8575064954522,17.2839286222097,11.7672763922841));
#187595=CARTESIAN_POINT('Ctrl Pts',(17.8762116340555,17.2755537423078,11.7660616256793));
#187596=CARTESIAN_POINT('Ctrl Pts',(17.883537153945,17.2723236366138,11.765585676383));
#187597=CARTESIAN_POINT('Ctrl Pts',(17.8967322209495,17.2665945997368,11.7647279263509));
#187598=CARTESIAN_POINT('Ctrl Pts',(17.9025951013253,17.2640804876699,11.7643466498865));
#187599=CARTESIAN_POINT('Ctrl Pts',(17.9150971771305,17.2587861349701,11.7635332360662));
#187600=CARTESIAN_POINT('Ctrl Pts',(17.921739354713,17.2560131841253,11.7631008565504));
#187601=CARTESIAN_POINT('Ctrl Pts',(17.9396435883359,17.2486455888189,11.7619346948704));
#187602=CARTESIAN_POINT('Ctrl Pts',(17.9509311878002,17.2441140934168,11.7611987885809));
#187603=CARTESIAN_POINT('Ctrl Pts',(18.0072712518788,17.2220577795327,11.7575216494345));
#187604=CARTESIAN_POINT('Ctrl Pts',(18.052872674146,17.205983592002,11.7545322703025));
#187605=CARTESIAN_POINT('Ctrl Pts',(18.185439394958,17.1642991658036,11.7457982236481));
#187606=CARTESIAN_POINT('Ctrl Pts',(18.2735446935313,17.1426961494182,11.7399361871599));
#187607=CARTESIAN_POINT('Ctrl Pts',(18.521323084779,17.0985608225958,11.7234139787401));
#187608=CARTESIAN_POINT('Ctrl Pts',(18.6826001408388,17.088503163016,11.7125879234403));
#187609=CARTESIAN_POINT('Ctrl Pts',(18.8634453702092,17.097866469298,11.7012278450611));
#187610=CARTESIAN_POINT('Ctrl Pts',(18.8834143387194,17.0991844671051,11.6999848858957));
#187611=CARTESIAN_POINT('Ctrl Pts',(18.9097243575146,17.101296066981,11.6983649308391));
#187612=CARTESIAN_POINT('Ctrl Pts',(18.9160840370131,17.1018354401103,11.6979747208991));
#187613=CARTESIAN_POINT('Ctrl Pts',(18.926345008534,17.1027524437223,11.6973474534102));
#187614=CARTESIAN_POINT('Ctrl Pts',(18.9302478042486,17.1031121565025,11.6971094107527));
#187615=CARTESIAN_POINT('Ctrl Pts',(18.9377537164033,17.1038249883426,11.6966526736526));
#187616=CARTESIAN_POINT('Ctrl Pts',(18.9413569292791,17.1041765117315,11.6964338952279));
#187617=CARTESIAN_POINT('Ctrl Pts',(18.9498789862241,17.1050299836163,11.6959175573198));
#187618=CARTESIAN_POINT('Ctrl Pts',(18.9547970419502,17.1055399281874,11.6956204467097));
#187619=CARTESIAN_POINT('Ctrl Pts',(18.9711038049876,17.1072885129879,11.6946380612876));
#187620=CARTESIAN_POINT('Ctrl Pts',(18.9824844704968,17.1086023887075,11.6939568833196));
#187621=CARTESIAN_POINT('Ctrl Pts',(19.1109324947416,17.1244890590825,11.6863133149267));
#187622=CARTESIAN_POINT('Ctrl Pts',(19.2266129258574,17.1487327291917,11.6798419021154));
#187623=CARTESIAN_POINT('Ctrl Pts',(19.5086719421455,17.2329516115556,11.6638230600567));
#187624=CARTESIAN_POINT('Ctrl Pts',(19.6706728924389,17.304319827775,11.6543458740009));
#187625=CARTESIAN_POINT('Ctrl Pts',(19.8416151672737,17.4067263706571,11.6427658792243));
#187626=CARTESIAN_POINT('Ctrl Pts',(19.8610904185327,17.4188276264973,11.641422579047));
#187627=CARTESIAN_POINT('Ctrl Pts',(19.8883814409061,17.4364061254231,11.6395041256385));
#187628=CARTESIAN_POINT('Ctrl Pts',(19.8963630560191,17.441623823978,11.6389386005849));
#187629=CARTESIAN_POINT('Ctrl Pts',(19.9092796865872,17.4501927308181,11.638016031709));
#187630=CARTESIAN_POINT('Ctrl Pts',(19.9142363246372,17.453511223992,11.637660219825));
#187631=CARTESIAN_POINT('Ctrl Pts',(19.9245865375435,17.4605042732831,11.6369134495187));
#187632=CARTESIAN_POINT('Ctrl Pts',(19.9299772703034,17.4641829059483,11.6365223392293));
#187633=CARTESIAN_POINT('Ctrl Pts',(19.9427688964197,17.472998872286,11.6355890554431));
#187634=CARTESIAN_POINT('Ctrl Pts',(19.9501541300167,17.4781586070825,11.635046031337));
#187635=CARTESIAN_POINT('Ctrl Pts',(19.9749601424897,17.4957261561287,11.6332077271044));
#187636=CARTESIAN_POINT('Ctrl Pts',(19.9922253197168,17.5083504685743,11.6319041429512));
#187637=CARTESIAN_POINT('Ctrl Pts',(20.0854145658999,17.5786820065511,11.6247326934401));
#187638=CARTESIAN_POINT('Ctrl Pts',(20.1575544480654,17.6412000611845,11.6186752640702));
#187639=CARTESIAN_POINT('Ctrl Pts',(20.3463173134782,17.8285292930982,11.601393168069));
#187640=CARTESIAN_POINT('Ctrl Pts',(20.4524301921778,17.9628866480319,11.5898824037791));
#187641=CARTESIAN_POINT('Ctrl Pts',(20.5603509505221,18.1397979273546,11.5766576666444));
#187642=CARTESIAN_POINT('Ctrl Pts',(20.57861949941,18.1715718157039,11.5743529639277));
#187643=CARTESIAN_POINT('Ctrl Pts',(20.5994487038554,18.2100799178343,11.5716570035792));
#187644=CARTESIAN_POINT('Ctrl Pts',(20.602810589737,18.21637099349,11.5712196051305));
#187645=CARTESIAN_POINT('Ctrl Pts',(20.6082459609496,18.226667020723,11.5705088550857));
#187646=CARTESIAN_POINT('Ctrl Pts',(20.6103385276089,18.2306617589275,11.5702343378718));
#187647=CARTESIAN_POINT('Ctrl Pts',(20.6140628232737,18.2378270990376,11.5697442062462));
#187648=CARTESIAN_POINT('Ctrl Pts',(20.6156993150121,18.2409951530477,11.5695282946073));
#187649=CARTESIAN_POINT('Ctrl Pts',(20.6192276530486,18.2478681290267,11.5690616039283));
#187650=CARTESIAN_POINT('Ctrl Pts',(20.6211165800761,18.2515744851269,11.5688110087091));
#187651=CARTESIAN_POINT('Ctrl Pts',(20.626366437074,18.2619509741536,11.5681123636846));
#187652=CARTESIAN_POINT('Ctrl Pts',(20.6297030491524,18.2686334371222,11.5676658133312));
#187653=CARTESIAN_POINT('Ctrl Pts',(20.6489484254469,18.3076933513134,11.5650744951055));
#187654=CARTESIAN_POINT('Ctrl Pts',(20.6640639132924,18.3404576321502,11.5629759692517));
#187655=CARTESIAN_POINT('Ctrl Pts',(20.7101041284028,18.4473563975019,11.5563185937797));
#187656=CARTESIAN_POINT('Ctrl Pts',(20.7376520855221,18.5228725301513,11.5519018029582));
#187657=CARTESIAN_POINT('Ctrl Pts',(20.814350346623,18.7772073608206,11.5374210755901));
#187658=CARTESIAN_POINT('Ctrl Pts',(20.8443233527318,18.9608741795873,11.5275076728548));
#187659=CARTESIAN_POINT('Ctrl Pts',(20.850683492793,19.1682208228441,11.5154430554136));
#187660=CARTESIAN_POINT('Ctrl Pts',(20.8510150821734,19.1903565020096,11.514145375606));
#187661=CARTESIAN_POINT('Ctrl Pts',(20.8509935059029,19.2209564225428,11.5123365701689));
#187662=CARTESIAN_POINT('Ctrl Pts',(20.8509367816855,19.229419923203,11.5118347054949));
#187663=CARTESIAN_POINT('Ctrl Pts',(20.8507521095536,19.2439615597,11.5109696283486));
#187664=CARTESIAN_POINT('Ctrl Pts',(20.8506487283448,19.2500399452842,11.5106071882997));
#187665=CARTESIAN_POINT('Ctrl Pts',(20.8503817373643,19.262564760712,11.5098585984424));
#187666=CARTESIAN_POINT('Ctrl Pts',(20.8502148518894,19.2690110507754,11.5094723497967));
#187667=CARTESIAN_POINT('Ctrl Pts',(20.8497582249999,19.2840015033914,11.5085718683574));
#187668=CARTESIAN_POINT('Ctrl Pts',(20.8494461760307,19.2925448288995,11.508056941505));
#187669=CARTESIAN_POINT('Ctrl Pts',(20.8482832880671,19.3198476914612,11.506405690706));
#187670=CARTESIAN_POINT('Ctrl Pts',(20.8472346028292,19.3385974916544,11.5052631939268));
#187671=CARTESIAN_POINT('Ctrl Pts',(20.8407644072337,19.4319796143988,11.4995290342648));
#187672=CARTESIAN_POINT('Ctrl Pts',(20.8316385705084,19.5062940176621,11.4948225831321));
#187673=CARTESIAN_POINT('Ctrl Pts',(20.7996299614578,19.687139086067,11.483024051358));
#187674=CARTESIAN_POINT('Ctrl Pts',(20.7724244874635,19.7926852207526,11.4758315175729));
#187675=CARTESIAN_POINT('Ctrl Pts',(20.6984130390039,20.0092325456473,11.4607128992608));
#187676=CARTESIAN_POINT('Ctrl Pts',(20.6500047460643,20.1193095677476,11.4528146158638));
#187677=CARTESIAN_POINT('Ctrl Pts',(20.5879671131522,20.2330496086128,11.4448124904301));
#187678=CARTESIAN_POINT('Ctrl Pts',(20.5833565701869,20.241368741364,11.4442282413917));
#187679=CARTESIAN_POINT('Ctrl Pts',(20.5764411833575,20.2536507062563,11.443367551538));
#187680=CARTESIAN_POINT('Ctrl Pts',(20.5741793569393,20.257637446586,11.443088464346));
#187681=CARTESIAN_POINT('Ctrl Pts',(20.5701318464466,20.2647179898275,11.4425933662205));
#187682=CARTESIAN_POINT('Ctrl Pts',(20.568351266249,20.2678146442444,11.4423770326644));
#187683=CARTESIAN_POINT('Ctrl Pts',(20.564505999401,20.2744630521267,11.4419130028762));
#187684=CARTESIAN_POINT('Ctrl Pts',(20.5624388157592,20.2780132964338,11.4416654714748));
#187685=CARTESIAN_POINT('Ctrl Pts',(20.5567036949756,20.2877973596427,11.4409839591826));
#187686=CARTESIAN_POINT('Ctrl Pts',(20.5530140856026,20.2940185008691,11.440551360865));
#187687=CARTESIAN_POINT('Ctrl Pts',(20.5326181655577,20.3280102918894,11.4381910441826));
#187688=CARTESIAN_POINT('Ctrl Pts',(20.5153067554257,20.3554150470175,11.436300466029));
#187689=CARTESIAN_POINT('Ctrl Pts',(20.4072947045071,20.5180096149243,11.4250911199681));
#187690=CARTESIAN_POINT('Ctrl Pts',(20.3018689459553,20.6427779714588,11.416486910597));
#187691=CARTESIAN_POINT('Ctrl Pts',(20.09793873662,20.8342779509002,11.4011722330067));
#187692=CARTESIAN_POINT('Ctrl Pts',(20.006231539933,20.9071078444334,11.3946449646661));
#187693=CARTESIAN_POINT('Ctrl Pts',(19.8971257895582,20.9799066663237,11.386960711716));
#187694=CARTESIAN_POINT('Ctrl Pts',(19.8851829588666,20.9877020506805,11.3861208407895));
#187695=CARTESIAN_POINT('Ctrl Pts',(19.8660430767335,20.9999211319645,11.3847763911939));
#187696=CARTESIAN_POINT('Ctrl Pts',(19.8588966067553,21.0044235319427,11.384274739009));
#187697=CARTESIAN_POINT('Ctrl Pts',(19.8462410710984,21.0122913348911,11.3833868836638));
#187698=CARTESIAN_POINT('Ctrl Pts',(19.840743166652,21.0156745510025,11.3830013438486));
#187699=CARTESIAN_POINT('Ctrl Pts',(19.8293356543442,21.0226225973459,11.3822016999385));
#187700=CARTESIAN_POINT('Ctrl Pts',(19.8234239229801,21.0261837772457,11.3817874680774));
#187701=CARTESIAN_POINT('Ctrl Pts',(19.8081959275306,21.0352558129019,11.3807208267198));
#187702=CARTESIAN_POINT('Ctrl Pts',(19.7988547052325,21.040724190024,11.3800668814504));
#187703=CARTESIAN_POINT('Ctrl Pts',(19.7596174765505,21.0632915349395,11.3773212180823));
#187704=CARTESIAN_POINT('Ctrl Pts',(19.7293497752228,21.0797305168827,11.3752059633401));
#187705=CARTESIAN_POINT('Ctrl Pts',(19.6493784143508,21.1206703889558,11.369620985308));
#187706=CARTESIAN_POINT('Ctrl Pts',(19.5990925190084,21.1439699263036,11.3661123489404));
#187707=CARTESIAN_POINT('Ctrl Pts',(19.4467384063022,21.2074254863261,11.3555014376942));
#187708=CARTESIAN_POINT('Ctrl Pts',(19.3424074793955,21.2416520229834,11.3482509136916));
#187709=CARTESIAN_POINT('Ctrl Pts',(19.1747107431891,21.2825768883695,11.3368488670876));
#187710=CARTESIAN_POINT('Ctrl Pts',(19.1128778844095,21.2947727674556,11.3326994998946));
#187711=CARTESIAN_POINT('Ctrl Pts',(19.0438800960324,21.3052085363039,11.3281829746019));
#187712=CARTESIAN_POINT('Ctrl Pts',(19.0371642199998,21.30619128596,11.3277445549054));
#187713=CARTESIAN_POINT('Ctrl Pts',(19.024295039637,21.3080112903441,11.3269068594373));
#187714=CARTESIAN_POINT('Ctrl Pts',(19.0181425530176,21.3088538015726,11.3265074312346));
#187715=CARTESIAN_POINT('Ctrl Pts',(18.9688108796419,21.3153881967183,11.3233136428653));
#187716=CARTESIAN_POINT('Ctrl Pts',(18.9254656145631,21.3197738974488,11.320561820466));
#187717=CARTESIAN_POINT('Ctrl Pts',(18.8745136451574,21.3233450067153,11.3174139063159));
#187718=CARTESIAN_POINT('Ctrl Pts',(18.8670117286538,21.3238306595101,11.3169526273957));
#187719=CARTESIAN_POINT('Ctrl Pts',(18.8548894646491,21.3245505994799,11.3162109846748));
#187720=CARTESIAN_POINT('Ctrl Pts',(18.8502707344577,21.3248097162401,11.3159292844753));
#187721=CARTESIAN_POINT('Ctrl Pts',(18.8420797806199,21.3252423113772,11.3154313066971));
#187722=CARTESIAN_POINT('Ctrl Pts',(18.838507932476,21.3254218791267,11.3152146920184));
#187723=CARTESIAN_POINT('Ctrl Pts',(18.8308592081091,21.3257869746991,11.314752000603));
#187724=CARTESIAN_POINT('Ctrl Pts',(18.8267822566414,21.3259697652809,11.3145060785246));
#187725=CARTESIAN_POINT('Ctrl Pts',(18.815601521543,21.3264386628916,11.3138335222304));
#187726=CARTESIAN_POINT('Ctrl Pts',(18.8084967102127,21.3267007794601,11.3134082111764));
#187727=CARTESIAN_POINT('Ctrl Pts',(18.7707404119018,21.3279032875953,11.3111583671086));
#187728=CARTESIAN_POINT('Ctrl Pts',(18.7400708072438,21.328213440811,11.309366993464));
#187729=CARTESIAN_POINT('Ctrl Pts',(18.647516376947,21.3271380201154,11.3040413601126));
#187730=CARTESIAN_POINT('Ctrl Pts',(18.5856858241574,21.323705269713,11.3005915993964));
#187731=CARTESIAN_POINT('Ctrl Pts',(18.3776128451735,21.3029717840945,11.2890938563863));
#187732=CARTESIAN_POINT('Ctrl Pts',(18.2330600690706,21.27313910069,11.2812648274557));
#187733=CARTESIAN_POINT('Ctrl Pts',(18.0216914871102,21.2059606560408,11.2688802993139));
#187734=CARTESIAN_POINT('Ctrl Pts',(17.9518634479933,21.1796320398422,11.2646305106726));
#187735=CARTESIAN_POINT('Ctrl Pts',(17.8715560718002,21.1444041776926,11.2594850483937));
#187736=CARTESIAN_POINT('Ctrl Pts',(17.8595869076564,21.1390204812067,11.2587112955402));
#187737=CARTESIAN_POINT('Ctrl Pts',(17.8402224192874,21.1300929809537,11.2574479303016));
#187738=CARTESIAN_POINT('Ctrl Pts',(17.8327961548068,21.1266168353431,11.2569606475912));
#187739=CARTESIAN_POINT('Ctrl Pts',(17.8196096840524,21.120350756607,11.256090354038));
#187740=CARTESIAN_POINT('Ctrl Pts',(17.813841553171,21.1175776650832,11.2557079311689));
#187741=CARTESIAN_POINT('Ctrl Pts',(17.8080207710294,21.1147466934437,11.2553202426781));
#187742=CARTESIAN_POINT('Ctrl Pts',(17.8079554093732,21.1147149002549,11.2553158890908));
#187743=CARTESIAN_POINT('Ctrl Pts',(17.8078339885017,21.1146558310345,11.255307801109));
#187744=CARTESIAN_POINT('Ctrl Pts',(17.8077779250923,21.1146285540619,11.2553040664948));
#187745=CARTESIAN_POINT('Ctrl Pts',(17.8076538533986,21.1145681817042,11.2552958011998));
#187746=CARTESIAN_POINT('Ctrl Pts',(17.8075858444125,21.114535084533,11.2552912703936));
#187747=CARTESIAN_POINT('Ctrl Pts',(17.807452159529,21.1144700167466,11.2552823637298));
#187748=CARTESIAN_POINT('Ctrl Pts',(17.8073864863653,21.1144380477662,11.2552779880711));
#187749=CARTESIAN_POINT('Ctrl Pts',(17.8072573926156,21.1143751980715,11.2552693863875));
#187750=CARTESIAN_POINT('Ctrl Pts',(17.8071939715084,21.1143443173864,11.2552651603432));
#187751=CARTESIAN_POINT('Ctrl Pts',(17.8070693003332,21.1142836054189,11.2552568525009));
#187752=CARTESIAN_POINT('Ctrl Pts',(17.8070080496665,21.1142537741084,11.2552527706773));
#187753=CARTESIAN_POINT('Ctrl Pts',(17.8068876406461,21.1141951233289,11.2552447460723));
#187754=CARTESIAN_POINT('Ctrl Pts',(17.8068284817233,21.114166303828,11.2552408032664));
#187755=CARTESIAN_POINT('Ctrl Pts',(17.8067121810781,21.1141096408034,11.2552330517305));
#187756=CARTESIAN_POINT('Ctrl Pts',(17.8066550384826,21.1140817970828,11.2552292429547));
#187757=CARTESIAN_POINT('Ctrl Pts',(17.8065426972086,21.1140270505878,11.2552217546312));
#187758=CARTESIAN_POINT('Ctrl Pts',(17.806487497978,21.1140001477569,11.2552180750583));
#187759=CARTESIAN_POINT('Ctrl Pts',(17.806378973743,21.1139472497063,11.2552108405295));
#187760=CARTESIAN_POINT('Ctrl Pts',(17.8063256479171,21.113921254284,11.2552072855296));
#187761=CARTESIAN_POINT('Ctrl Pts',(17.806220803362,21.1138701389139,11.2552002957034));
#187762=CARTESIAN_POINT('Ctrl Pts',(17.8061692836892,21.1138450186903,11.2551968608243));
#187763=CARTESIAN_POINT('Ctrl Pts',(17.8060679863102,21.1137956225081,11.2551901069273));
#187764=CARTESIAN_POINT('Ctrl Pts',(17.8060182078432,21.1137713463502,11.2551867878681));
#187765=CARTESIAN_POINT('Ctrl Pts',(17.8059203308769,21.1137236085736,11.2551802615048));
#187766=CARTESIAN_POINT('Ctrl Pts',(17.8058722313404,21.1137001466089,11.2551770541403));
#187767=CARTESIAN_POINT('Ctrl Pts',(17.8057776524382,21.1136540085261,11.255170747205));
#187768=CARTESIAN_POINT('Ctrl Pts',(17.8057311719284,21.1136313319989,11.255167647566));
#187769=CARTESIAN_POINT('Ctrl Pts',(17.8056397731782,21.1135867369853,11.2551615522446));
#187770=CARTESIAN_POINT('Ctrl Pts',(17.8055948538635,21.1135648181136,11.2551585564981));
#187771=CARTESIAN_POINT('Ctrl Pts',(17.8055065277404,21.1135217145418,11.2551526656655));
#187772=CARTESIAN_POINT('Ctrl Pts',(17.8054631194813,21.1135005292644,11.2551497704899));
#187773=CARTESIAN_POINT('Ctrl Pts',(17.8053777363302,21.1134588546397,11.2551440755411));
#187774=CARTESIAN_POINT('Ctrl Pts',(17.8053357757297,21.1134383723897,11.2551412767281));
#187775=CARTESIAN_POINT('Ctrl Pts',(17.805253255661,21.1133980884444,11.2551357723743));
#187776=CARTESIAN_POINT('Ctrl Pts',(17.805212696102,21.1133782868176,11.2551330668337));
#187777=CARTESIAN_POINT('Ctrl Pts',(17.8051329288425,21.1133393403973,11.2551277457562));
#187778=CARTESIAN_POINT('Ctrl Pts',(17.805093720955,21.1133201956176,11.2551251302126));
#187779=CARTESIAN_POINT('Ctrl Pts',(17.79846621008,21.1100838012974,11.2546829975794));
#187780=CARTESIAN_POINT('Ctrl Pts',(17.791894730149,21.1068323804713,11.2542422885588));
#187781=CARTESIAN_POINT('Ctrl Pts',(17.7737379027954,21.0977310738973,11.2530181240525));
#187782=CARTESIAN_POINT('Ctrl Pts',(17.7621894045932,21.0918087609933,11.2522321343146));
#187783=CARTESIAN_POINT('Ctrl Pts',(17.7365723286292,21.0783728613398,11.2504718796223));
#187784=CARTESIAN_POINT('Ctrl Pts',(17.7225328455187,21.0708057792333,11.2494957571305));
#187785=CARTESIAN_POINT('Ctrl Pts',(17.6793927687354,21.0469209289685,11.2464604104779));
#187786=CARTESIAN_POINT('Ctrl Pts',(17.6505924926393,21.0300739535338,11.2443827273179));
#187787=CARTESIAN_POINT('Ctrl Pts',(17.539088083641,20.9612610312077,11.2361333383974));
#187788=CARTESIAN_POINT('Ctrl Pts',(17.459630917763,20.9042831492104,11.2297928851541));
#187789=CARTESIAN_POINT('Ctrl Pts',(17.2624186334956,20.7410991442357,11.2129477485755));
#187790=CARTESIAN_POINT('Ctrl Pts',(17.1521409148208,20.6267976799242,11.2023305703547));
#187791=CARTESIAN_POINT('Ctrl Pts',(17.0467431035819,20.489696998505,11.1915593608907));
#187792=CARTESIAN_POINT('Ctrl Pts',(17.0379707577474,20.4780385490817,11.1906576667491));
#187793=CARTESIAN_POINT('Ctrl Pts',(17.0259863703975,20.4617637812291,11.1894195867916));
#187794=CARTESIAN_POINT('Ctrl Pts',(17.0226713707513,20.457224265418,11.1890764455044));
#187795=CARTESIAN_POINT('Ctrl Pts',(17.0173930949866,20.4499354887966,11.1885290657091));
#187796=CARTESIAN_POINT('Ctrl Pts',(17.0154182778975,20.4471946758364,11.1883240381722));
#187797=CARTESIAN_POINT('Ctrl Pts',(17.0113191227705,20.4414767251303,11.1878979983809));
#187798=CARTESIAN_POINT('Ctrl Pts',(17.0091959336214,20.438498801897,11.1876770699764));
#187799=CARTESIAN_POINT('Ctrl Pts',(17.0040988612963,20.4313104611357,11.1871460343829));
#187800=CARTESIAN_POINT('Ctrl Pts',(17.0011325936524,20.4270946198962,11.1868364487473));
#187801=CARTESIAN_POINT('Ctrl Pts',(16.9909116500558,20.4124546577151,11.1857676402282));
#187802=CARTESIAN_POINT('Ctrl Pts',(16.9837352337982,20.4019758839497,11.1850135678328));
#187803=CARTESIAN_POINT('Ctrl Pts',(16.9426473012017,20.3408070180423,11.1806708939601));
#187804=CARTESIAN_POINT('Ctrl Pts',(16.9108415162874,20.2887304468159,11.1772070877362));
#187805=CARTESIAN_POINT('Ctrl Pts',(16.828339396904,20.1395141436943,11.1677104439598));
#187806=CARTESIAN_POINT('Ctrl Pts',(16.7829144564847,20.0397971661308,11.1618386287765));
#187807=CARTESIAN_POINT('Ctrl Pts',(16.745419285258,19.9371100060985,11.1558808557757));
#187808=CARTESIAN_POINT('',(16.6169841362445,19.2120754279768,11.689056243827));
#187809=CARTESIAN_POINT('Ctrl Pts',(16.6170002731508,19.2120754164278,11.6890562436246));
#187810=CARTESIAN_POINT('Ctrl Pts',(16.6169638390757,19.1403535001558,11.6847206650338));
#187811=CARTESIAN_POINT('Ctrl Pts',(16.6205764456709,19.0684835617616,11.6803850864429));
#187812=CARTESIAN_POINT('Ctrl Pts',(16.6278569147558,18.9968731579697,11.6760495078521));
#187813=CARTESIAN_POINT('Ctrl Pts',(16.6351262827892,18.9253719436775,11.6717205400277));
#187814=CARTESIAN_POINT('Ctrl Pts',(16.6460523594264,18.8541299663727,11.6673915722033));
#187815=CARTESIAN_POINT('Ctrl Pts',(16.660601956967,18.7835546173521,11.663062604379));
#187816=CARTESIAN_POINT('Ctrl Pts',(16.6751392352658,18.7130390249528,11.6587373019207));
#187817=CARTESIAN_POINT('Ctrl Pts',(16.6932938534713,18.6431894242013,11.6544119994624));
#187818=CARTESIAN_POINT('Ctrl Pts',(16.7149810087479,18.5744064774415,11.6500866970042));
#187819=CARTESIAN_POINT('Ctrl Pts',(16.7366573538935,18.5056578160759,11.6457635505265));
#187820=CARTESIAN_POINT('Ctrl Pts',(16.7618625956119,18.4379752252655,11.6414404040489));
#187821=CARTESIAN_POINT('Ctrl Pts',(16.7904616388557,18.3717457841867,11.6371172575712));
#187822=CARTESIAN_POINT('Ctrl Pts',(16.8190563851715,18.3055262939003,11.6327947606345));
#187823=CARTESIAN_POINT('Ctrl Pts',(16.8510437238671,18.2407599735886,11.6284722636978));
#187824=CARTESIAN_POINT('Ctrl Pts',(16.8862405216007,18.1778137099316,11.6241497667611));
#187825=CARTESIAN_POINT('Ctrl Pts',(16.9214689659605,18.1148108491688,11.6198233833218));
#187826=CARTESIAN_POINT('Ctrl Pts',(16.9599123931251,18.0536317475416,11.6154969998825));
#187827=CARTESIAN_POINT('Ctrl Pts',(17.001342278154,17.994617568802,11.6111706164432));
#187828=CARTESIAN_POINT('Ctrl Pts',(17.042789639319,17.9355784964421,11.6068424080298));
#187829=CARTESIAN_POINT('Ctrl Pts',(17.0872256618387,17.8787065557693,11.6025141996164));
#187830=CARTESIAN_POINT('Ctrl Pts',(17.134380883397,17.8243105315903,11.5981859912031));
#187831=CARTESIAN_POINT('Ctrl Pts',(17.1816225942449,17.7698147374743,11.5938498442485));
#187832=CARTESIAN_POINT('Ctrl Pts',(17.231593123781,17.7178042891481,11.5895136972939));
#187833=CARTESIAN_POINT('Ctrl Pts',(17.283985843864,17.6685513146282,11.5851775503393));
#187834=CARTESIAN_POINT('Ctrl Pts',(17.333038486034,17.6224382567243,11.5811178362297));
#187835=CARTESIAN_POINT('Ctrl Pts',(17.3842137273592,17.5787421229118,11.5770581221201));
#187836=CARTESIAN_POINT('Ctrl Pts',(17.4372361998845,17.5376522636613,11.5729984080105));
#187837=CARTESIAN_POINT('Ctrl Pts',(17.494549025663,17.4932375875375,11.5686101990796));
#187838=CARTESIAN_POINT('Ctrl Pts',(17.5542581954977,17.4516841015565,11.5642219901487));
#187839=CARTESIAN_POINT('Ctrl Pts',(17.6160462231312,17.4132602099345,11.5598337812178));
#187840=CARTESIAN_POINT('Ctrl Pts',(17.677742547087,17.3748933457384,11.5554520851166));
#187841=CARTESIAN_POINT('Ctrl Pts',(17.7415111977163,17.3396471078963,11.5510703890153));
#187842=CARTESIAN_POINT('Ctrl Pts',(17.8070029012394,17.3077487346939,11.5466886929141));
#187843=CARTESIAN_POINT('Ctrl Pts',(17.872417646799,17.2758878446184,11.5423121456544));
#187844=CARTESIAN_POINT('Ctrl Pts',(17.9395509916038,17.2473672144278,11.5379355983948));
#187845=CARTESIAN_POINT('Ctrl Pts',(18.0080275301098,17.2223690707018,11.5335590511351));
#187846=CARTESIAN_POINT('Ctrl Pts',(18.0764606417902,17.1973867804352,11.5291852794182));
#187847=CARTESIAN_POINT('Ctrl Pts',(18.1462348050098,17.1759227092789,11.5248115077012));
#187848=CARTESIAN_POINT('Ctrl Pts',(18.2169543269185,17.158111115538,11.5204377359842));
#187849=CARTESIAN_POINT('Ctrl Pts',(18.2876523286392,17.1403049419248,11.5160652952207));
#187850=CARTESIAN_POINT('Ctrl Pts',(18.3592946504355,17.1261491568769,11.5116928544571));
#187851=CARTESIAN_POINT('Ctrl Pts',(18.4314717388384,17.1157277858955,11.5073204136936));
#187852=CARTESIAN_POINT('Ctrl Pts',(18.5036506728172,17.1053061484385,11.5029478611262));
#187853=CARTESIAN_POINT('Ctrl Pts',(18.5763639228386,17.0986191815878,11.4985753085589));
#187854=CARTESIAN_POINT('Ctrl Pts',(18.6491947479431,17.0956992957918,11.4942027559916));
#187855=CARTESIAN_POINT('Ctrl Pts',(18.722101159625,17.0927763796282,11.4898256654242));
#187856=CARTESIAN_POINT('Ctrl Pts',(18.7951249069972,17.0936283697016,11.4854485748569));
#187857=CARTESIAN_POINT('Ctrl Pts',(18.8678480060374,17.0982355286782,11.4810714842896));
#187858=CARTESIAN_POINT('Ctrl Pts',(18.9406108218611,17.1028452037952,11.4766920032306));
#187859=CARTESIAN_POINT('Ctrl Pts',(19.0130721829172,17.1112140756296,11.4723125221717));
#187860=CARTESIAN_POINT('Ctrl Pts',(19.0848207051458,17.1232706514395,11.4679330411128));
#187861=CARTESIAN_POINT('Ctrl Pts',(19.1566964011484,17.135348597449,11.4635457974531));
#187862=CARTESIAN_POINT('Ctrl Pts',(19.2278562638068,17.1511271959047,11.4591585537933));
#187863=CARTESIAN_POINT('Ctrl Pts',(19.297901126223,17.1704842515079,11.4547713101336));
#187864=CARTESIAN_POINT('Ctrl Pts',(19.3455248831594,17.1836451840766,11.4517884071988));
#187865=CARTESIAN_POINT('Ctrl Pts',(19.3926335158207,17.1984592758342,11.448805504264));
#187866=CARTESIAN_POINT('Ctrl Pts',(19.4391069833084,17.2148754692931,11.4458226013291));
#187867=CARTESIAN_POINT('Ctrl Pts',(19.5074750427239,17.2390256640267,11.4414343923982));
#187868=CARTESIAN_POINT('Ctrl Pts',(19.5747343896097,17.2667395128394,11.4370461834673));
#187869=CARTESIAN_POINT('Ctrl Pts',(19.6404874892065,17.2978953421435,11.4326579745364));
#187870=CARTESIAN_POINT('Ctrl Pts',(19.7061430003017,17.3290049310313,11.4282762784352));
#187871=CARTESIAN_POINT('Ctrl Pts',(19.7702962696066,17.3635461545568,11.4238945823339));
#187872=CARTESIAN_POINT('Ctrl Pts',(19.8325671704118,17.4013483285191,11.4195128862326));
#187873=CARTESIAN_POINT('Ctrl Pts',(19.8947648979526,17.4391060819186,11.415136338973));
#187874=CARTESIAN_POINT('Ctrl Pts',(19.9550842407136,17.4801169246317,11.4107597917133));
#187875=CARTESIAN_POINT('Ctrl Pts',(20.0131687750781,17.5241638357964,11.4063832444537));
#187876=CARTESIAN_POINT('Ctrl Pts',(20.0712164730752,17.5681828130502,11.4020094727367));
#187877=CARTESIAN_POINT('Ctrl Pts',(20.1270317913338,17.6152337476986,11.3976357010197));
#187878=CARTESIAN_POINT('Ctrl Pts',(20.1802876588314,17.6650565961485,11.3932619293028));
#187879=CARTESIAN_POINT('Ctrl Pts',(20.2335273203896,17.7148642833382,11.3888894885392));
#187880=CARTESIAN_POINT('Ctrl Pts',(20.2842087253976,17.7674418803648,11.3845170477756));
#187881=CARTESIAN_POINT('Ctrl Pts',(20.3320395381809,17.8224904989844,11.3801446070121));
#187882=CARTESIAN_POINT('Ctrl Pts',(20.3798715740033,17.8775405252032,11.3757720544448));
#187883=CARTESIAN_POINT('Ctrl Pts',(20.42485255801,17.935061333022,11.3713995018774));
#187884=CARTESIAN_POINT('Ctrl Pts',(20.4667296641656,17.9947200524055,11.3670269493101));
#187885=CARTESIAN_POINT('Ctrl Pts',(20.5086502319617,18.0544406878584,11.3626498587428));
#187886=CARTESIAN_POINT('Ctrl Pts',(20.5474602125879,18.1163032692072,11.3582727681754));
#187887=CARTESIAN_POINT('Ctrl Pts',(20.5829499551952,18.1799456545924,11.3538956776081));
#187888=CARTESIAN_POINT('Ctrl Pts',(20.618459080068,18.2436227974464,11.3495161965492));
#187889=CARTESIAN_POINT('Ctrl Pts',(20.6506441436593,18.3090812464314,11.3451367154902));
#187890=CARTESIAN_POINT('Ctrl Pts',(20.6793425856617,18.3759363949906,11.3407572344313));
#187891=CARTESIAN_POINT('Ctrl Pts',(20.7080918954598,18.442910043852,11.3363699907715));
#187892=CARTESIAN_POINT('Ctrl Pts',(20.7333420751794,18.5112848831346,11.3319827471118));
#187893=CARTESIAN_POINT('Ctrl Pts',(20.7549798102576,18.5806591346493,11.3275955034521));
#187894=CARTESIAN_POINT('Ctrl Pts',(20.7696913851037,18.6278269407924,11.3246126005173));
#187895=CARTESIAN_POINT('Ctrl Pts',(20.78273408769,18.6754564326547,11.3216296975824));
#187896=CARTESIAN_POINT('Ctrl Pts',(20.7940858734221,18.7234190383877,11.3186467946476));
#187897=CARTESIAN_POINT('Ctrl Pts',(20.8107857153611,18.7939777992408,11.3142585857167));
#187898=CARTESIAN_POINT('Ctrl Pts',(20.8238889631162,18.865533246677,11.3098703767858));
#187899=CARTESIAN_POINT('Ctrl Pts',(20.8332827468939,18.9376852572697,11.3054821678549));
#187900=CARTESIAN_POINT('Ctrl Pts',(20.8426625887389,19.0097301823156,11.3011004717537));
#187901=CARTESIAN_POINT('Ctrl Pts',(20.8483438339329,19.0823694384942,11.2967187756524));
#187902=CARTESIAN_POINT('Ctrl Pts',(20.8502642454991,19.1551910112784,11.2923370795511));
#187903=CARTESIAN_POINT('Ctrl Pts',(20.8521824004289,19.2279270129192,11.2879605322915));
#187904=CARTESIAN_POINT('Ctrl Pts',(20.8503484880034,19.3008444257667,11.2835839850318));
#187905=CARTESIAN_POINT('Ctrl Pts',(20.8447520630799,19.3735260846882,11.2792074377722));
#187906=CARTESIAN_POINT('Ctrl Pts',(20.8391591873277,19.4461616499579,11.2748336660552));
#187907=CARTESIAN_POINT('Ctrl Pts',(20.8298085704124,19.5185612781815,11.2704598943383));
#187908=CARTESIAN_POINT('Ctrl Pts',(20.8167418305018,19.5903091977241,11.2660861226213));
#187909=CARTESIAN_POINT('Ctrl Pts',(20.803679066844,19.6620352841338,11.2617136818577));
#187910=CARTESIAN_POINT('Ctrl Pts',(20.7869025116117,19.7331095812968,11.2573412410942));
#187911=CARTESIAN_POINT('Ctrl Pts',(20.7665052467619,19.8031244986364,11.2529688003306));
#187912=CARTESIAN_POINT('Ctrl Pts',(20.7461074603517,19.8731412062653,11.2485962477633));
#187913=CARTESIAN_POINT('Ctrl Pts',(20.7220889173522,19.9420980177239,11.244223695196));
#187914=CARTESIAN_POINT('Ctrl Pts',(20.6945926588476,20.0096021700903,11.2398511426286));
#187915=CARTESIAN_POINT('Ctrl Pts',(20.6670678636887,20.0771763808123,11.2354740520613));
#187916=CARTESIAN_POINT('Ctrl Pts',(20.6360583291635,20.1432944746739,11.231096961494));
#187917=CARTESIAN_POINT('Ctrl Pts',(20.6017550792375,20.2075841479687,11.2267198709267));
#187918=CARTESIAN_POINT('Ctrl Pts',(20.5674330950335,20.2719089322403,11.2223403898677));
#187919=CARTESIAN_POINT('Ctrl Pts',(20.5298140629451,20.3344028942418,11.2179609088088));
#187920=CARTESIAN_POINT('Ctrl Pts',(20.4891333854102,20.3947211662459,11.2135814277498));
#187921=CARTESIAN_POINT('Ctrl Pts',(20.4483806016475,20.4551463519821,11.2091941840901));
#187922=CARTESIAN_POINT('Ctrl Pts',(20.4045556257383,20.513387760871,11.2048069404304));
#187923=CARTESIAN_POINT('Ctrl Pts',(20.3579349545335,20.5691326383842,11.2004196967707));
#187924=CARTESIAN_POINT('Ctrl Pts',(20.3262373904715,20.6070337835293,11.1974367938359));
#187925=CARTESIAN_POINT('Ctrl Pts',(20.2932482928816,20.643781572932,11.194453890901));
#187926=CARTESIAN_POINT('Ctrl Pts',(20.2590638380205,20.6792878770739,11.1914709879662));
#187927=CARTESIAN_POINT('Ctrl Pts',(20.208774394013,20.7315219203344,11.1870827790353));
#187928=CARTESIAN_POINT('Ctrl Pts',(20.1557001261013,20.7812712846033,11.1826945701045));
#187929=CARTESIAN_POINT('Ctrl Pts',(20.1001163804878,20.8282244850246,11.1783063611736));
#187930=CARTESIAN_POINT('Ctrl Pts',(20.0446151303686,20.8751079991115,11.1739246650723));
#187931=CARTESIAN_POINT('Ctrl Pts',(19.9866121616041,20.9192032789,11.169542968971));
#187932=CARTESIAN_POINT('Ctrl Pts',(19.9264202255136,20.9602349772932,11.1651612728697));
#187933=CARTESIAN_POINT('Ctrl Pts',(19.8662990197384,21.0012184601753,11.1607847256101));
#187934=CARTESIAN_POINT('Ctrl Pts',(19.8039943529514,21.0391452426346,11.1564081783505));
#187935=CARTESIAN_POINT('Ctrl Pts',(19.7398513412539,21.0737807383849,11.1520316310908));
#187936=CARTESIAN_POINT('Ctrl Pts',(19.6757490081222,21.1083942688071,11.1476578593739));
#187937=CARTESIAN_POINT('Ctrl Pts',(19.609811066688,21.1397204253384,11.1432840876569));
#187938=CARTESIAN_POINT('Ctrl Pts',(19.5424096422239,21.1675691529715,11.1389103159399));
#187939=CARTESIAN_POINT('Ctrl Pts',(19.4750287282396,21.1954094061432,11.1345378751764));
#187940=CARTESIAN_POINT('Ctrl Pts',(19.4061856609221,21.2197741471639,11.1301654344128));
#187941=CARTESIAN_POINT('Ctrl Pts',(19.3362735429419,21.2405210221804,11.1257929936493));
#187942=CARTESIAN_POINT('Ctrl Pts',(19.2663596373011,21.2612684276968,11.1214204410819));
#187943=CARTESIAN_POINT('Ctrl Pts',(19.1953770897385,21.2783976482242,11.1170478885146));
#187944=CARTESIAN_POINT('Ctrl Pts',(19.1237335771413,21.2918163635575,11.1126753359473));
#187945=CARTESIAN_POINT('Ctrl Pts',(19.0520157102043,21.3052490053397,11.1082982453799));
#187946=CARTESIAN_POINT('Ctrl Pts',(18.9796359837857,21.3149633643477,11.1039211548126));
#187947=CARTESIAN_POINT('Ctrl Pts',(18.9070108440337,21.3209185405713,11.0995440642453));
#187948=CARTESIAN_POINT('Ctrl Pts',(18.8343460409976,21.3268769691377,11.0951645831863));
#187949=CARTESIAN_POINT('Ctrl Pts',(18.7614360402703,21.329072112832,11.0907851021274));
#187950=CARTESIAN_POINT('Ctrl Pts',(18.6886982399089,21.3275152374913,11.0864056210685));
#187951=CARTESIAN_POINT('Ctrl Pts',(18.6158315122846,21.3259556025994,11.0820183774087));
#187952=CARTESIAN_POINT('Ctrl Pts',(18.5431380760587,21.3206307033085,11.077631133749));
#187953=CARTESIAN_POINT('Ctrl Pts',(18.4710305707961,21.3116037416191,11.0732438900893));
#187954=CARTESIAN_POINT('Ctrl Pts',(18.42200441548,21.3054662775062,11.0702609871545));
#187955=CARTESIAN_POINT('Ctrl Pts',(18.3732489672181,21.2976185484977,11.0672780842196));
#187956=CARTESIAN_POINT('Ctrl Pts',(18.324890387372,21.2880937207684,11.0642951812848));
#187957=CARTESIAN_POINT('Ctrl Pts',(18.2537491009801,21.2740815537551,11.0599069723539));
#187958=CARTESIAN_POINT('Ctrl Pts',(18.1831896640501,21.2563828809338,11.055518763423));
#187959=CARTESIAN_POINT('Ctrl Pts',(18.1136230257294,21.2350606240414,11.0511305544921));
#187960=CARTESIAN_POINT('Ctrl Pts',(18.0441596358343,21.2137700129135,11.0467488583908));
#187961=CARTESIAN_POINT('Ctrl Pts',(17.9756865768824,21.1888666339678,11.0423671622896));
#187962=CARTESIAN_POINT('Ctrl Pts',(17.9086046585653,21.1604644214086,11.0379854661883));
#187963=CARTESIAN_POINT('Ctrl Pts',(17.8416015668409,21.1320955837095,11.0336089189286));
#187964=CARTESIAN_POINT('Ctrl Pts',(17.7759868104058,21.1002362668759,11.029232371669));
#187965=CARTESIAN_POINT('Ctrl Pts',(17.7121444440024,21.0650496818254,11.0248558244094));
#187966=CARTESIAN_POINT('Ctrl Pts',(17.6483425654999,21.0298854115958,11.0204820526924));
#187967=CARTESIAN_POINT('Ctrl Pts',(17.5863112682425,20.9913982921379,11.0161082809754));
#187968=CARTESIAN_POINT('Ctrl Pts',(17.5264117827665,20.9497983487451,11.0117345092584));
#187969=CARTESIAN_POINT('Ctrl Pts',(17.4665305249049,20.9082110643548,11.0073620684949));
#187970=CARTESIAN_POINT('Ctrl Pts',(17.4087801868834,20.863513111593,11.0029896277313));
#187971=CARTESIAN_POINT('Ctrl Pts',(17.3534932447841,20.8159579741549,10.9986171869678));
#187972=CARTESIAN_POINT('Ctrl Pts',(17.2982048889917,20.7684016207268,10.9942446344004));
#187973=CARTESIAN_POINT('Ctrl Pts',(17.245380418581,20.7179882536485,10.9898720818331));
#187974=CARTESIAN_POINT('Ctrl Pts',(17.1953181280013,20.6650106934898,10.9854995292658));
#187975=CARTESIAN_POINT('Ctrl Pts',(17.145203880888,20.6119781512208,10.9811224386984));
#187976=CARTESIAN_POINT('Ctrl Pts',(17.0978578691726,20.5563764539264,10.9767453481311));
#187977=CARTESIAN_POINT('Ctrl Pts',(17.0535398976926,20.4985336285134,10.9723682575638));
#187978=CARTESIAN_POINT('Ctrl Pts',(17.0091977225236,20.4406592129868,10.9679887765048));
#187979=CARTESIAN_POINT('Ctrl Pts',(16.9678871535196,20.3805416302804,10.9636092954459));
#187980=CARTESIAN_POINT('Ctrl Pts',(16.9298246475462,20.3185379440895,10.9592298143869));
#187981=CARTESIAN_POINT('Ctrl Pts',(16.8916946760364,20.256424356781,10.9548425707272));
#187982=CARTESIAN_POINT('Ctrl Pts',(16.8568244953674,20.1924184139091,10.9504553270675));
#187983=CARTESIAN_POINT('Ctrl Pts',(16.8253843166289,20.1269012900908,10.9460680834078));
#187984=CARTESIAN_POINT('Ctrl Pts',(16.8040080246552,20.0823559591094,10.943085180473));
#187985=CARTESIAN_POINT('Ctrl Pts',(16.7842163233974,20.0371125159699,10.9401022775382));
#187986=CARTESIAN_POINT('Ctrl Pts',(16.7660496141036,19.9912949946335,10.9371193746033));
#187987=CARTESIAN_POINT('Ctrl Pts',(16.7589277812078,19.9733333084868,10.9359499973704));
#187988=CARTESIAN_POINT('Ctrl Pts',(16.7520500861352,19.9552696214365,10.9347806201374));
#187989=CARTESIAN_POINT('Ctrl Pts',(16.7454193623258,19.9371102171621,10.9336112429045));
#187990=CARTESIAN_POINT('Ctrl Pts',(16.7460270442577,19.9368788012273,11.7337477294316));
#187991=CARTESIAN_POINT('Ctrl Pts',(16.6804602657827,19.7626326020608,11.7225565578517));
#187992=CARTESIAN_POINT('Ctrl Pts',(16.623583940577,19.5201104597515,11.7076594077154));
#187993=CARTESIAN_POINT('Ctrl Pts',(16.613796038846,19.2734660709366,11.692762257579));
#187994=CARTESIAN_POINT('Ctrl Pts',(16.6141771432254,19.2120774369074,11.6890562790225));
#187995=CARTESIAN_POINT('Origin',(18.734,19.211,0.));
#187996=CARTESIAN_POINT('',(16.745419226499,19.9371098451765,12.7565300941239));
#187997=CARTESIAN_POINT('',(16.7454193728684,19.937110246035,12.5316746173356));
#187998=CARTESIAN_POINT('',(16.7454193623258,19.9371102171621,0.));
#187999=CARTESIAN_POINT('',(16.6170000980014,19.2116441567485,12.7090269805744));
#188000=CARTESIAN_POINT('Ctrl Pts',(16.745419226499,19.9371098451765,12.7565300941239));
#188001=CARTESIAN_POINT('Ctrl Pts',(16.7109718279897,19.8427695262457,12.7499960896148));
#188002=CARTESIAN_POINT('Ctrl Pts',(16.6832543081821,19.7460230012717,12.7433224418381));
#188003=CARTESIAN_POINT('Ctrl Pts',(16.6461765008723,19.5701016041718,12.7314741686189));
#188004=CARTESIAN_POINT('Ctrl Pts',(16.6342037280546,19.4917464784093,12.7262975863649));
#188005=CARTESIAN_POINT('Ctrl Pts',(16.6241532252603,19.386842951453,12.7196400353508));
#188006=CARTESIAN_POINT('Ctrl Pts',(16.6221401933133,19.3607413040614,12.718006033714));
#188007=CARTESIAN_POINT('Ctrl Pts',(16.6202046974363,19.3276490764454,12.7159684458409));
#188008=CARTESIAN_POINT('Ctrl Pts',(16.6198320659138,19.3206883666375,12.7155417585203));
#188009=CARTESIAN_POINT('Ctrl Pts',(16.6192953232568,19.3096400680818,12.7148676617419));
#188010=CARTESIAN_POINT('Ctrl Pts',(16.6191086713618,19.3055536967893,12.7146190224069));
#188011=CARTESIAN_POINT('Ctrl Pts',(16.6187836658417,19.2979552364133,12.7141579923509));
#188012=CARTESIAN_POINT('Ctrl Pts',(16.6186422157249,19.2944433828792,12.713945435868));
#188013=CARTESIAN_POINT('Ctrl Pts',(16.6183781730345,19.2874551180024,12.713523492419));
#188014=CARTESIAN_POINT('Ctrl Pts',(16.6182554032475,19.2839787743982,12.7133140970092));
#188015=CARTESIAN_POINT('Ctrl Pts',(16.6179937470186,19.2760131516113,12.7128354112316));
#188016=CARTESIAN_POINT('Ctrl Pts',(16.6178605771198,19.271523683795,12.7125664352002));
#188017=CARTESIAN_POINT('Ctrl Pts',(16.6175253046709,19.258861266542,12.7118100059682));
#188018=CARTESIAN_POINT('Ctrl Pts',(16.6173562534074,19.2506874230827,12.7113243118677));
#188019=CARTESIAN_POINT('Ctrl Pts',(16.6170813858816,19.2322240481652,12.7102326610896));
#188020=CARTESIAN_POINT('Ctrl Pts',(16.6170032290586,19.2219342728014,12.7096280997442));
#188021=CARTESIAN_POINT('Ctrl Pts',(16.6170000980014,19.2116441567485,12.7090269805744));
#188022=CARTESIAN_POINT('Ctrl Pts',(16.6170000985846,19.211646070454,12.7090270923677));
#188023=CARTESIAN_POINT('Ctrl Pts',(16.6169387604032,19.0106572727102,12.6972858928636));
#188024=CARTESIAN_POINT('Ctrl Pts',(16.6454993147949,18.8106400257173,12.6868416498719));
#188025=CARTESIAN_POINT('Ctrl Pts',(16.7265384440085,18.5331076467323,12.670879152307));
#188026=CARTESIAN_POINT('Ctrl Pts',(16.756460397437,18.4502276826733,12.6659226579821));
#188027=CARTESIAN_POINT('Ctrl Pts',(16.7995990705701,18.3506500116555,12.659597648559));
#188028=CARTESIAN_POINT('Ctrl Pts',(16.8080187647746,18.33196342723,12.6583942839193));
#188029=CARTESIAN_POINT('Ctrl Pts',(16.8204632172919,18.305381750612,12.6566576096086));
#188030=CARTESIAN_POINT('Ctrl Pts',(16.8242684544766,18.2973847348022,12.6561318718541));
#188031=CARTESIAN_POINT('Ctrl Pts',(16.8309529273847,18.2835610117046,12.6552172998102));
#188032=CARTESIAN_POINT('Ctrl Pts',(16.8338090432712,18.2777232114141,12.6548292737635));
#188033=CARTESIAN_POINT('Ctrl Pts',(16.8393529180669,18.266522675095,12.6540812910053));
#188034=CARTESIAN_POINT('Ctrl Pts',(16.8420366812202,18.2611580228387,12.6537214770087));
#188035=CARTESIAN_POINT('Ctrl Pts',(16.8491284285195,18.2471314310087,12.652776568871));
#188036=CARTESIAN_POINT('Ctrl Pts',(16.8535732884557,18.2384883872946,12.6521901818696));
#188037=CARTESIAN_POINT('Ctrl Pts',(16.8692136681454,18.2085837554897,12.6501466771834));
#188038=CARTESIAN_POINT('Ctrl Pts',(16.8807112218679,18.1874830138528,12.6486789112992));
#188039=CARTESIAN_POINT('Ctrl Pts',(16.9645641503801,18.0396400157092,12.6382064943479));
#188040=CARTESIAN_POINT('Ctrl Pts',(17.0494840526099,17.9205041437133,12.6287343676895));
#188041=CARTESIAN_POINT('Ctrl Pts',(17.2364708926923,17.708392449996,12.6100727414369));
#188042=CARTESIAN_POINT('Ctrl Pts',(17.336731979102,17.6147323021957,12.6009553692923));
#188043=CARTESIAN_POINT('Ctrl Pts',(17.4554189558392,17.5236704857472,12.5915872424048));
#188044=CARTESIAN_POINT('Ctrl Pts',(17.4655673061445,17.5160283500168,12.5907967765417));
#188045=CARTESIAN_POINT('Ctrl Pts',(17.4812019684215,17.5044738568522,12.5895957983659));
#188046=CARTESIAN_POINT('Ctrl Pts',(17.4866390061365,17.5004957062644,12.5891812225684));
#188047=CARTESIAN_POINT('Ctrl Pts',(17.4956289991096,17.4939836033656,12.5885009017715));
#188048=CARTESIAN_POINT('Ctrl Pts',(17.4991709183665,17.4914345949975,12.5882341773707));
#188049=CARTESIAN_POINT('Ctrl Pts',(17.5060326408267,17.4865285618955,12.5877200253526));
#188050=CARTESIAN_POINT('Ctrl Pts',(17.5093514085005,17.4841701288151,12.5874725034557));
#188051=CARTESIAN_POINT('Ctrl Pts',(17.5126866850503,17.4818144151458,12.5872249234406));
#188052=CARTESIAN_POINT('Ctrl Pts',(17.5126963787218,17.481807568605,12.5872242038822));
#188053=CARTESIAN_POINT('Ctrl Pts',(17.5127158007082,17.4817938512999,12.5872227622137));
#188054=CARTESIAN_POINT('Ctrl Pts',(17.5127255285653,17.4817869808599,12.5872220401377));
#188055=CARTESIAN_POINT('Ctrl Pts',(17.5127450188822,17.4817732157876,12.5872205934371));
#188056=CARTESIAN_POINT('Ctrl Pts',(17.5127547816535,17.4817663209362,12.5872198687896));
#188057=CARTESIAN_POINT('Ctrl Pts',(17.5127749744187,17.481752060271,12.5872183699903));
#188058=CARTESIAN_POINT('Ctrl Pts',(17.5127854044269,17.4817446944647,12.5872175958389));
#188059=CARTESIAN_POINT('Ctrl Pts',(17.5128064327553,17.4817298442729,12.5872160350666));
#188060=CARTESIAN_POINT('Ctrl Pts',(17.5128170307833,17.4817223600985,12.5872152484677));
#188061=CARTESIAN_POINT('Ctrl Pts',(17.5128383984912,17.4817072708259,12.5872136625536));
#188062=CARTESIAN_POINT('Ctrl Pts',(17.5128491683808,17.4816996655845,12.5872128632233));
#188063=CARTESIAN_POINT('Ctrl Pts',(17.5128708834199,17.4816843316445,12.5872112515796));
#188064=CARTESIAN_POINT('Ctrl Pts',(17.5128818286274,17.4816766029099,12.5872104392624));
#188065=CARTESIAN_POINT('Ctrl Pts',(17.5129038985387,17.4816610190072,12.5872088013319));
#188066=CARTESIAN_POINT('Ctrl Pts',(17.5129150226881,17.4816531642355,12.5872079757601));
#188067=CARTESIAN_POINT('Ctrl Pts',(17.51293745395,17.4816373258262,12.5872063110645));
#188068=CARTESIAN_POINT('Ctrl Pts',(17.5129487614422,17.4816293419258,12.5872054719128));
#188069=CARTESIAN_POINT('Ctrl Pts',(17.5129715632085,17.4816132425786,12.5872037797753));
#188070=CARTESIAN_POINT('Ctrl Pts',(17.5129830576609,17.4816051270115,12.5872029267766));
#188071=CARTESIAN_POINT('Ctrl Pts',(17.51300623779,17.4815887612113,12.5872012066167));
#188072=CARTESIAN_POINT('Ctrl Pts',(17.5130179232493,17.4815805111373,12.587200339472));
#188073=CARTESIAN_POINT('Ctrl Pts',(17.5130414893778,17.4815638735268,12.5871985907259));
#188074=CARTESIAN_POINT('Ctrl Pts',(17.5130533703946,17.4815554857508,12.587197709099));
#188075=CARTESIAN_POINT('Ctrl Pts',(17.513077332228,17.4815385695139,12.5871959310493));
#188076=CARTESIAN_POINT('Ctrl Pts',(17.5130894127562,17.4815300412627,12.5871950346484));
#188077=CARTESIAN_POINT('Ctrl Pts',(17.5131137781087,17.4815128409201,12.5871932267183));
#188078=CARTESIAN_POINT('Ctrl Pts',(17.5131260629415,17.4815041688291,12.5871923151891));
#188079=CARTESIAN_POINT('Ctrl Pts',(17.5131508412232,17.4814866777767,12.5871904766836));
#188080=CARTESIAN_POINT('Ctrl Pts',(17.5131633349751,17.4814778586081,12.5871895496854));
#188081=CARTESIAN_POINT('Ctrl Pts',(17.5131885363069,17.4814600697418,12.5871876798568));
#188082=CARTESIAN_POINT('Ctrl Pts',(17.5132012433539,17.4814511004273,12.5871867370666));
#188083=CARTESIAN_POINT('Ctrl Pts',(17.5132268759753,17.481433007973,12.5871848353069));
#188084=CARTESIAN_POINT('Ctrl Pts',(17.5132398017299,17.4814238847134,12.5871838763248));
#188085=CARTESIAN_POINT('Ctrl Pts',(17.5132658766755,17.4814054809262,12.587181941819));
#188086=CARTESIAN_POINT('Ctrl Pts',(17.5132790258933,17.4813962003872,12.587180966294));
#188087=CARTESIAN_POINT('Ctrl Pts',(17.5161295888974,17.4793843605113,12.5869694903282));
#188088=CARTESIAN_POINT('Ctrl Pts',(17.5189718855124,17.4773888145413,12.5867594811754));
#188089=CARTESIAN_POINT('Ctrl Pts',(17.5255910720128,17.4727658298507,12.5862723713935));
#188090=CARTESIAN_POINT('Ctrl Pts',(17.5293716209543,17.4701437058654,12.5859956347871));
#188091=CARTESIAN_POINT('Ctrl Pts',(17.5410660208189,17.4620890068941,12.5851440493046));
#188092=CARTESIAN_POINT('Ctrl Pts',(17.549008422291,17.4566978284536,12.5845719401235));
#188093=CARTESIAN_POINT('Ctrl Pts',(17.6515087940936,17.3881359171802,12.5772648276371));
#188094=CARTESIAN_POINT('Ctrl Pts',(17.7509851461404,17.3326204316007,12.5709971427924));
#188095=CARTESIAN_POINT('Ctrl Pts',(17.9581449953138,17.2379989222324,12.5585849310954));
#188096=CARTESIAN_POINT('Ctrl Pts',(18.0654897152336,17.199091093247,12.5524565708601));
#188097=CARTESIAN_POINT('Ctrl Pts',(18.2285727248127,17.1544820277548,12.5430552207825));
#188098=CARTESIAN_POINT('Ctrl Pts',(18.2822455064783,17.1420292090627,12.5399492838202));
#188099=CARTESIAN_POINT('Ctrl Pts',(18.3700241107728,17.1252419459907,12.5348076541231));
#188100=CARTESIAN_POINT('Ctrl Pts',(18.4038581131141,17.119619774897,12.5328113012355));
#188101=CARTESIAN_POINT('Ctrl Pts',(18.4485134975469,17.1133100189139,12.5301515219491));
#188102=CARTESIAN_POINT('Ctrl Pts',(18.4592258646563,17.1118799539278,12.5295116042883));
#188103=CARTESIAN_POINT('Ctrl Pts',(18.4767925395974,17.1096716338146,12.528459006155));
#188104=CARTESIAN_POINT('Ctrl Pts',(18.4836406159394,17.1088447352054,12.5280478663419));
#188105=CARTESIAN_POINT('Ctrl Pts',(18.4969066602564,17.1073086156269,12.5272498089319));
#188106=CARTESIAN_POINT('Ctrl Pts',(18.5033240794254,17.1065952597776,12.5268630265715));
#188107=CARTESIAN_POINT('Ctrl Pts',(18.5181525792627,17.1050155776359,12.5259675885405));
#188108=CARTESIAN_POINT('Ctrl Pts',(18.526565745182,17.1041702672102,12.5254582764669));
#188109=CARTESIAN_POINT('Ctrl Pts',(18.54921315962,17.1020317432914,12.5240837390301));
#188110=CARTESIAN_POINT('Ctrl Pts',(18.563455623542,17.1008322616166,12.523215584082));
#188111=CARTESIAN_POINT('Ctrl Pts',(18.6944563158825,17.091134448096,12.5151947707832));
#188112=CARTESIAN_POINT('Ctrl Pts',(18.8117001618678,17.0921917270833,12.5077391494698));
#188113=CARTESIAN_POINT('Ctrl Pts',(19.0909641228782,17.1179234122904,12.4894190486677));
#188114=CARTESIAN_POINT('Ctrl Pts',(19.2514009456122,17.1517065704701,12.4784127146827));
#188115=CARTESIAN_POINT('Ctrl Pts',(19.4364131370526,17.2136743690216,12.466024206083));
#188116=CARTESIAN_POINT('Ctrl Pts',(19.466243901464,17.2244167497298,12.4640385147701));
#188117=CARTESIAN_POINT('Ctrl Pts',(19.5025262506239,17.2384108369186,12.4616474974234));
#188118=CARTESIAN_POINT('Ctrl Pts',(19.5092155104863,17.241030071317,12.4612076935512));
#188119=CARTESIAN_POINT('Ctrl Pts',(19.5196990585668,17.2451966584612,12.4605201762969));
#188120=CARTESIAN_POINT('Ctrl Pts',(19.523502335295,17.2467210352245,12.4602711189686));
#188121=CARTESIAN_POINT('Ctrl Pts',(19.530614520113,17.2495956363273,12.4598060927066));
#188122=CARTESIAN_POINT('Ctrl Pts',(19.5339243974569,17.2509431819302,12.4595899729136));
#188123=CARTESIAN_POINT('Ctrl Pts',(19.5414871061499,17.2540445240389,12.4590968198226));
#188124=CARTESIAN_POINT('Ctrl Pts',(19.545737635987,17.2558038019854,12.4588201220291));
#188125=CARTESIAN_POINT('Ctrl Pts',(19.5588366369341,17.2612755070236,12.4579687748242));
#188126=CARTESIAN_POINT('Ctrl Pts',(19.5676657700213,17.2650343096884,12.4573968628904));
#188127=CARTESIAN_POINT('Ctrl Pts',(19.6520261986637,17.3016283824231,12.4519480306099));
#188128=CARTESIAN_POINT('Ctrl Pts',(19.7256155647243,17.3387890425237,12.4473145497081));
#188129=CARTESIAN_POINT('Ctrl Pts',(19.9204061040629,17.4518702878759,12.434893169299));
#188130=CARTESIAN_POINT('Ctrl Pts',(20.0363750951913,17.5359127117115,12.4272971835306));
#188131=CARTESIAN_POINT('Ctrl Pts',(20.2010418772366,17.6827573998835,12.4150448484645));
#188132=CARTESIAN_POINT('Ctrl Pts',(20.2561837109088,17.7376730856162,12.4106413581722));
#188133=CARTESIAN_POINT('Ctrl Pts',(20.3209966749389,17.8097512020768,12.4049837749805));
#188134=CARTESIAN_POINT('Ctrl Pts',(20.3336224808072,17.8241818709403,12.4038569177371));
#188135=CARTESIAN_POINT('Ctrl Pts',(20.3516384812304,17.8453466504768,12.4022115767129));
#188136=CARTESIAN_POINT('Ctrl Pts',(20.3571865105103,17.8519455949942,12.4016995951999));
#188137=CARTESIAN_POINT('Ctrl Pts',(20.3668207842451,17.8635479542822,12.4008011007121));
#188138=CARTESIAN_POINT('Ctrl Pts',(20.3709247486381,17.8685365573542,12.400415316153));
#188139=CARTESIAN_POINT('Ctrl Pts',(20.3788333443386,17.8782400911947,12.399665907595));
#188140=CARTESIAN_POINT('Ctrl Pts',(20.3826406981208,17.8829527295762,12.3993023989869));
#188141=CARTESIAN_POINT('Ctrl Pts',(20.3916688730864,17.8942262120945,12.3984338560035));
#188142=CARTESIAN_POINT('Ctrl Pts',(20.3968710193114,17.9008018198436,12.3979280801225));
#188143=CARTESIAN_POINT('Ctrl Pts',(20.4153602060731,17.9244599831696,12.3961111953677));
#188144=CARTESIAN_POINT('Ctrl Pts',(20.42842383789,17.9417147048461,12.3947913005092));
#188145=CARTESIAN_POINT('Ctrl Pts',(20.5535656086143,18.1123799843618,12.3817826321626));
#188146=CARTESIAN_POINT('Ctrl Pts',(20.6447543120481,18.2799933909853,12.3692503567173));
#188147=CARTESIAN_POINT('Ctrl Pts',(20.7398679353733,18.529708054316,12.3516166715367));
#188148=CARTESIAN_POINT('Ctrl Pts',(20.763408153841,18.6034071612342,12.3465444579389));
#188149=CARTESIAN_POINT('Ctrl Pts',(20.7917370738072,18.7123518968674,12.3393736389055));
#188150=CARTESIAN_POINT('Ctrl Pts',(20.7997559561205,18.7466892608215,12.3371599363058));
#188151=CARTESIAN_POINT('Ctrl Pts',(20.8084200500398,18.7884772292334,12.3345346319601));
#188152=CARTESIAN_POINT('Ctrl Pts',(20.8098879861357,18.7957493424596,12.3340802687922));
#188153=CARTESIAN_POINT('Ctrl Pts',(20.8121172312758,18.8071002767284,12.333375119713));
#188154=CARTESIAN_POINT('Ctrl Pts',(20.8129048118116,18.8111737908877,12.3331228760275));
#188155=CARTESIAN_POINT('Ctrl Pts',(20.814347221162,18.818753696663,12.3326550522728));
#188156=CARTESIAN_POINT('Ctrl Pts',(20.815005157165,18.8222593934293,12.3324393022404));
#188157=CARTESIAN_POINT('Ctrl Pts',(20.8164775991352,18.8302159122948,12.331951023367));
#188158=CARTESIAN_POINT('Ctrl Pts',(20.8172866964435,18.8346676819031,12.3316788046212));
#188159=CARTESIAN_POINT('Ctrl Pts',(20.8193431868608,18.8461926830013,12.3309765214122));
#188160=CARTESIAN_POINT('Ctrl Pts',(20.8205688797905,18.8532697961615,12.3305476600726));
#188161=CARTESIAN_POINT('Ctrl Pts',(20.8279613566092,18.8972847517752,12.3278944811131));
#188162=CARTESIAN_POINT('Ctrl Pts',(20.833183542551,18.9343770429387,12.3257200014894));
#188163=CARTESIAN_POINT('Ctrl Pts',(20.8565548960087,19.1397148363527,12.3139241909942));
#188164=CARTESIAN_POINT('Ctrl Pts',(20.8554669831909,19.3095411506274,12.3050166702248));
#188165=CARTESIAN_POINT('Ctrl Pts',(20.8221149301088,19.5724334827263,12.2904420727788));
#188166=CARTESIAN_POINT('Ctrl Pts',(20.803633726641,19.6664901328602,12.2850742117915));
#188167=CARTESIAN_POINT('Ctrl Pts',(20.7733042873709,19.7796707885036,12.278251486055));
#188168=CARTESIAN_POINT('Ctrl Pts',(20.7674421653872,19.8002888532445,12.276993800894));
#188169=CARTESIAN_POINT('Ctrl Pts',(20.7586707222561,19.8294486834147,12.2751925776329));
#188170=CARTESIAN_POINT('Ctrl Pts',(20.7560181930505,19.8380667673546,12.2746574199199));
#188171=CARTESIAN_POINT('Ctrl Pts',(20.7513506443056,19.8528940639882,12.2737317254693));
#188172=CARTESIAN_POINT('Ctrl Pts',(20.7493617991531,19.8591114321674,12.2733420524814));
#188173=CARTESIAN_POINT('Ctrl Pts',(20.7455011060697,19.8709908042675,12.2725945775596));
#188174=CARTESIAN_POINT('Ctrl Pts',(20.7436340245679,19.8766543003732,12.2722369359772));
#188175=CARTESIAN_POINT('Ctrl Pts',(20.7387220829723,19.8913448602326,12.2713058751967));
#188176=CARTESIAN_POINT('Ctrl Pts',(20.7356401979983,19.9003593198896,12.2707312357628));
#188177=CARTESIAN_POINT('Ctrl Pts',(20.7249522999965,19.9309452158217,12.2687700074478));
#188178=CARTESIAN_POINT('Ctrl Pts',(20.7170577833659,19.9524134730854,12.2673738818407));
#188179=CARTESIAN_POINT('Ctrl Pts',(20.6450122292029,20.1389450934458,12.255067323928));
#188180=CARTESIAN_POINT('Ctrl Pts',(20.5607424089589,20.2954528318668,12.2434385931731));
#188181=CARTESIAN_POINT('Ctrl Pts',(20.4274581620335,20.4824791282448,12.2282659895484));
#188182=CARTESIAN_POINT('Ctrl Pts',(20.3953206283761,20.5241922149986,12.2247947652309));
#188183=CARTESIAN_POINT('Ctrl Pts',(20.3176601832236,20.6175719432667,12.2168801295183));
#188184=CARTESIAN_POINT('Ctrl Pts',(20.2711010346898,20.6683080114399,12.212469773892));
#188185=CARTESIAN_POINT('Ctrl Pts',(20.2159399040907,20.7228264833275,12.2076863885666));
#188186=CARTESIAN_POINT('Ctrl Pts',(20.2096935108621,20.7289241954265,12.2071507375361));
#188187=CARTESIAN_POINT('Ctrl Pts',(20.2002227526364,20.7380558062979,12.2063478490094));
#188188=CARTESIAN_POINT('Ctrl Pts',(20.1970263842658,20.7411184253721,12.2060784464144));
#188189=CARTESIAN_POINT('Ctrl Pts',(20.1912657085946,20.7466034963174,12.2055957683517));
#188190=CARTESIAN_POINT('Ctrl Pts',(20.1887049480794,20.7490295699078,12.2053822146375));
#188191=CARTESIAN_POINT('Ctrl Pts',(20.1830738246341,20.754337871076,12.2049148182156));
#188192=CARTESIAN_POINT('Ctrl Pts',(20.1800009316714,20.7572173326706,12.2046611874514));
#188193=CARTESIAN_POINT('Ctrl Pts',(20.1714356858358,20.7651955512158,12.2039581134963));
#188194=CARTESIAN_POINT('Ctrl Pts',(20.1659247580008,20.7702743997007,12.2035101659433));
#188195=CARTESIAN_POINT('Ctrl Pts',(20.1366555825276,20.7969627129844,12.2011535421934));
#188196=CARTESIAN_POINT('Ctrl Pts',(20.1124334934574,20.8180599756423,12.1992809939189));
#188197=CARTESIAN_POINT('Ctrl Pts',(20.0728030321974,20.8510222149184,12.196321899611));
#188198=CARTESIAN_POINT('Ctrl Pts',(20.0576960547959,20.8632394564732,12.1952173029466));
#188199=CARTESIAN_POINT('Ctrl Pts',(20.0412884782937,20.8761390079734,12.1940399061242));
#188200=CARTESIAN_POINT('Ctrl Pts',(20.0401534162749,20.8770295119004,12.1939585680488));
#188201=CARTESIAN_POINT('Ctrl Pts',(20.0209795414295,20.8920405851875,12.1925864693753));
#188202=CARTESIAN_POINT('Ctrl Pts',(20.0027131474509,20.9058689599033,12.1913075600736));
#188203=CARTESIAN_POINT('Ctrl Pts',(19.9473641170615,20.9463740112137,12.1875044861132));
#188204=CARTESIAN_POINT('Ctrl Pts',(19.9096382839208,20.9721502778281,12.1850068003114));
#188205=CARTESIAN_POINT('Ctrl Pts',(19.7788706621966,21.055421779044,12.1765663179));
#188206=CARTESIAN_POINT('Ctrl Pts',(19.6822228710713,21.1069216499718,12.1706782218446));
#188207=CARTESIAN_POINT('Ctrl Pts',(19.5315382636709,21.1727999012095,12.161533872076));
#188208=CARTESIAN_POINT('Ctrl Pts',(19.4802032684083,21.1928945913558,12.1584263479471));
#188209=CARTESIAN_POINT('Ctrl Pts',(19.3957343138344,21.2222120018684,12.1532823251587));
#188210=CARTESIAN_POINT('Ctrl Pts',(19.3630560968352,21.2326711525379,12.1512852143881));
#188211=CARTESIAN_POINT('Ctrl Pts',(19.319767956074,21.2453750230576,12.1486245684813));
#188212=CARTESIAN_POINT('Ctrl Pts',(19.3093734290834,21.248339255831,12.1479845616418));
#188213=CARTESIAN_POINT('Ctrl Pts',(19.2923087977329,21.2530646099514,12.1469318541869));
#188214=CARTESIAN_POINT('Ctrl Pts',(19.2856518975241,21.2548729821268,12.1465206948594));
#188215=CARTESIAN_POINT('Ctrl Pts',(19.2727471256471,21.2583109742531,12.1457226262795));
#188216=CARTESIAN_POINT('Ctrl Pts',(19.2665003959816,21.2599446106562,12.1453358524049));
#188217=CARTESIAN_POINT('Ctrl Pts',(19.2520570055273,21.2636513150955,12.1444404729316));
#188218=CARTESIAN_POINT('Ctrl Pts',(19.2438552450985,21.2657038979243,12.1439312112001));
#188219=CARTESIAN_POINT('Ctrl Pts',(19.221758525465,21.2710934016981,12.1425568977084));
#188220=CARTESIAN_POINT('Ctrl Pts',(19.2078418965947,21.2743388098415,12.141688917848));
#188221=CARTESIAN_POINT('Ctrl Pts',(19.0798347076321,21.3028272338778,12.133681578609));
#188222=CARTESIAN_POINT('Ctrl Pts',(18.9638887178433,21.3187206151964,12.1262404356165));
#188223=CARTESIAN_POINT('Ctrl Pts',(18.6847502786384,21.3336733314719,12.1079811189833));
#188224=CARTESIAN_POINT('Ctrl Pts',(18.521803430621,21.3236145640143,12.0970228908445));
#188225=CARTESIAN_POINT('Ctrl Pts',(18.3296151316165,21.2892730227673,12.0846173735738));
#188226=CARTESIAN_POINT('Ctrl Pts',(18.2977462306467,21.2828177517052,12.0825798088158));
#188227=CARTESIAN_POINT('Ctrl Pts',(18.2589760858404,21.2740302215162,12.080135252125));
#188228=CARTESIAN_POINT('Ctrl Pts',(18.2519235718755,21.272393638985,12.0796919708425));
#188229=CARTESIAN_POINT('Ctrl Pts',(18.240880971458,21.2697713601372,12.0790002393744));
#188230=CARTESIAN_POINT('Ctrl Pts',(18.2368852009058,21.2688101872662,12.0787504184084));
#188231=CARTESIAN_POINT('Ctrl Pts',(18.2294218428266,21.2669918875424,12.0782847345719));
#188232=CARTESIAN_POINT('Ctrl Pts',(18.2259536637447,21.266137630132,12.0780687162314));
#188233=CARTESIAN_POINT('Ctrl Pts',(18.2180420293894,21.2641676407031,12.0775767898743));
#188234=CARTESIAN_POINT('Ctrl Pts',(18.2136000320197,21.2630462622705,12.0773012110212));
#188235=CARTESIAN_POINT('Ctrl Pts',(18.1999589566366,21.2595554422334,12.0764567167957));
#188236=CARTESIAN_POINT('Ctrl Pts',(18.1907720122815,21.2571384598475,12.075890475519));
#188237=CARTESIAN_POINT('Ctrl Pts',(18.1084484488737,21.2348865079895,12.0708364030099));
#188238=CARTESIAN_POINT('Ctrl Pts',(18.0364012526074,21.2111974708642,12.0665543442511));
#188239=CARTESIAN_POINT('Ctrl Pts',(17.9259496547316,21.1681842046639,12.0599935529638));
#188240=CARTESIAN_POINT('Ctrl Pts',(17.8866044167707,21.1514732111642,12.0576573773012));
#188241=CARTESIAN_POINT('Ctrl Pts',(17.7485094048649,21.0878187045986,12.0493787556857));
#188242=CARTESIAN_POINT('Ctrl Pts',(17.6529227037613,21.0344338912099,12.0434920554354));
#188243=CARTESIAN_POINT('Ctrl Pts',(17.516026117633,20.9434150677657,12.0343509506364));
#188244=CARTESIAN_POINT('Ctrl Pts',(17.4713725721059,20.9111451935431,12.0312452864231));
#188245=CARTESIAN_POINT('Ctrl Pts',(17.4010406358429,20.856018019602,12.0261040679831));
#188246=CARTESIAN_POINT('Ctrl Pts',(17.3745704123617,20.8342116162799,12.0241078453512));
#188247=CARTESIAN_POINT('Ctrl Pts',(17.3404706856775,20.8047006758762,12.0214482150112));
#188248=CARTESIAN_POINT('Ctrl Pts',(17.3323532455072,20.7975661546967,12.0208083126805));
#188249=CARTESIAN_POINT('Ctrl Pts',(17.3191448670055,20.7857766610118,12.0197557333397));
#188250=CARTESIAN_POINT('Ctrl Pts',(17.3140213609048,20.7811583494063,12.019344596881));
#188251=CARTESIAN_POINT('Ctrl Pts',(17.3041456373962,20.7721685349377,12.0185465413904));
#188252=CARTESIAN_POINT('Ctrl Pts',(17.2993906644874,20.767800162437,12.0181597575704));
#188253=CARTESIAN_POINT('Ctrl Pts',(17.288455178468,20.7576611353554,12.0172643094692));
#188254=CARTESIAN_POINT('Ctrl Pts',(17.2822891367916,20.7518750971701,12.0167549887386));
#188255=CARTESIAN_POINT('Ctrl Pts',(17.2657938223441,20.7362094669447,12.0153804127899));
#188256=CARTESIAN_POINT('Ctrl Pts',(17.2555298070371,20.7262620799574,12.0145122277316));
#188257=CARTESIAN_POINT('Ctrl Pts',(17.1621046131226,20.6338659212449,12.0064890650655));
#188258=CARTESIAN_POINT('Ctrl Pts',(17.0858314394438,20.5447672500487,11.9990309185508));
#188259=CARTESIAN_POINT('Ctrl Pts',(16.9216222700977,20.3172193719957,11.9806998283651));
#188260=CARTESIAN_POINT('Ctrl Pts',(16.8416122554602,20.1739658140329,11.9696846896713));
#188261=CARTESIAN_POINT('Ctrl Pts',(16.7671124243987,19.9945720871467,11.9573528861249));
#188262=CARTESIAN_POINT('Ctrl Pts',(16.7559529381101,19.9659582685393,11.9554288650358));
#188263=CARTESIAN_POINT('Ctrl Pts',(16.7454193623241,19.9371102171575,11.9535387334123));
#188264=CARTESIAN_POINT('',(16.6163526568764,19.2091064841458,12.4890562790225));
#188265=CARTESIAN_POINT('Ctrl Pts',(16.6163526568764,19.2091064841458,12.4890562790225));
#188266=CARTESIAN_POINT('Ctrl Pts',(16.6150299493055,19.0661177741218,12.4804472042752));
#188267=CARTESIAN_POINT('Ctrl Pts',(16.6934796238476,18.2204816490939,12.4294461939675));
#188268=CARTESIAN_POINT('Ctrl Pts',(17.8308508880792,16.8763369760823,12.336053248099));
#188269=CARTESIAN_POINT('Ctrl Pts',(20.2082246499765,17.1878857088602,12.2088774414178));
#188270=CARTESIAN_POINT('Ctrl Pts',(21.2330887962208,19.3555162351247,12.0817016347362));
#188271=CARTESIAN_POINT('Ctrl Pts',(19.9651940828767,21.3905620853514,11.9545258280549));
#188272=CARTESIAN_POINT('Ctrl Pts',(17.7787241911337,21.4228769879768,11.8385411929533));
#188273=CARTESIAN_POINT('Ctrl Pts',(16.9288259197432,20.4226737419889,11.7649484934122));
#188274=CARTESIAN_POINT('Ctrl Pts',(16.7460270442577,19.9368788012273,11.7337477294316));
#188275=CARTESIAN_POINT('Ctrl Pts',(16.6170008641598,19.2090871874988,12.489429316251));
#188276=CARTESIAN_POINT('Ctrl Pts',(16.6168618955398,19.3628902644884,12.4977918761832));
#188277=CARTESIAN_POINT('Ctrl Pts',(16.633483105635,19.5162417805676,12.5060812887087));
#188278=CARTESIAN_POINT('Ctrl Pts',(16.6718147732515,19.6902443673696,12.5163103612939));
#188279=CARTESIAN_POINT('Ctrl Pts',(16.6774689198822,19.7139541935533,12.5177213153689));
#188280=CARTESIAN_POINT('Ctrl Pts',(16.6866974527108,19.7498908469243,12.519888695236));
#188281=CARTESIAN_POINT('Ctrl Pts',(16.6899750038319,19.7621922256845,12.5206357860504));
#188282=CARTESIAN_POINT('Ctrl Pts',(16.6962720542647,19.7849976098997,12.5220308421496));
#188283=CARTESIAN_POINT('Ctrl Pts',(16.6992623441283,19.7955092830765,12.5226778527903));
#188284=CARTESIAN_POINT('Ctrl Pts',(16.7042800303639,19.8126425797401,12.5237391489304));
#188285=CARTESIAN_POINT('Ctrl Pts',(16.7062587868906,19.819278324291,12.5241518434894));
#188286=CARTESIAN_POINT('Ctrl Pts',(16.7101425344424,19.8320728766593,12.5249508170893));
#188287=CARTESIAN_POINT('Ctrl Pts',(16.7120431741991,19.8382329329575,12.5253369497411));
#188288=CARTESIAN_POINT('Ctrl Pts',(16.716482554786,19.8523912812155,12.5262278480922));
#188289=CARTESIAN_POINT('Ctrl Pts',(16.7190407627863,19.8603833125067,12.5267332492526));
#188290=CARTESIAN_POINT('Ctrl Pts',(16.7260160948594,19.8817366625947,12.5280904273584));
#188291=CARTESIAN_POINT('Ctrl Pts',(16.7305189854825,19.8950693263921,12.528945019885));
#188292=CARTESIAN_POINT('Ctrl Pts',(16.7385075449603,19.9179671007584,12.5304253836614));
#188293=CARTESIAN_POINT('Ctrl Pts',(16.7419293246322,19.9275521350618,12.5310489251602));
#188294=CARTESIAN_POINT('Ctrl Pts',(16.7454193728684,19.937110246035,12.5316746173356));
#188295=CARTESIAN_POINT('Origin',(18.734,19.211,0.));
#188296=CARTESIAN_POINT('',(16.7454193601307,19.9371102111504,13.5571444941232));
#188297=CARTESIAN_POINT('',(16.7454193976962,19.9371103140301,13.3344632337298));
#188298=CARTESIAN_POINT('',(16.7454193623258,19.9371102171621,0.));
#188299=CARTESIAN_POINT('Ctrl Pts',(16.7454193601307,19.9371102111504,13.5571444941232));
#188300=CARTESIAN_POINT('Ctrl Pts',(16.7397540738622,19.9215948273702,13.556205238638));
#188301=CARTESIAN_POINT('Ctrl Pts',(16.7342701797465,19.9060126210941,13.5552608618068));
#188302=CARTESIAN_POINT('Ctrl Pts',(16.7177768414227,19.8573354415282,13.5523054355895));
#188303=CARTESIAN_POINT('Ctrl Pts',(16.7074032797185,19.8240341387795,13.550275897431));
#188304=CARTESIAN_POINT('Ctrl Pts',(16.6948809080674,19.7800347670629,13.5475781926283));
#188305=CARTESIAN_POINT('Ctrl Pts',(16.6919850817183,19.7695537611094,13.5469343990448));
#188306=CARTESIAN_POINT('Ctrl Pts',(16.6873806778076,19.7523742988017,13.5458770486284));
#188307=CARTESIAN_POINT('Ctrl Pts',(16.6856239155965,19.7456888782045,13.5454650598561));
#188308=CARTESIAN_POINT('Ctrl Pts',(16.6822909632723,19.7327476849927,13.5446665086269));
#188309=CARTESIAN_POINT('Ctrl Pts',(16.6807105627297,19.7264930683827,13.5442800875236));
#188310=CARTESIAN_POINT('Ctrl Pts',(16.6771333674884,19.7120584351188,13.5433871593065));
#188311=CARTESIAN_POINT('Ctrl Pts',(16.675156748058,19.7038735741306,13.5428800073666));
#188312=CARTESIAN_POINT('Ctrl Pts',(16.6699846617209,19.6818826805959,13.5415150676855));
#188313=CARTESIAN_POINT('Ctrl Pts',(16.666878945586,19.6680561744549,13.5406544136644));
#188314=CARTESIAN_POINT('Ctrl Pts',(16.6325818101217,19.5078618808092,13.530652836331));
#188315=CARTESIAN_POINT('Ctrl Pts',(16.6168624938294,19.3586426934898,13.5210013133909));
#188316=CARTESIAN_POINT('Ctrl Pts',(16.6171394758123,19.0592697728877,13.5012717527447));
#188317=CARTESIAN_POINT('Ctrl Pts',(16.6331712117549,18.9099266964476,13.4912565952426));
#188318=CARTESIAN_POINT('Ctrl Pts',(16.6681544973136,18.7481628833701,13.4809318509259));
#188319=CARTESIAN_POINT('Ctrl Pts',(16.6716463803462,18.7328437301509,13.4799597589874));
#188320=CARTESIAN_POINT('Ctrl Pts',(16.6766589549459,18.711930477319,13.4786417905151));
#188321=CARTESIAN_POINT('Ctrl Pts',(16.6780324475907,18.706302081055,13.4782879916511));
#188322=CARTESIAN_POINT('Ctrl Pts',(16.6802514660739,18.6973682261554,13.4777279334526));
#188323=CARTESIAN_POINT('Ctrl Pts',(16.681081895107,18.6940590994209,13.4775208184102));
#188324=CARTESIAN_POINT('Ctrl Pts',(16.6828132681113,18.6872298273676,13.4770940882093));
#188325=CARTESIAN_POINT('Ctrl Pts',(16.6837152757193,18.6837099921797,13.4768745417128));
#188326=CARTESIAN_POINT('Ctrl Pts',(16.6858857804549,18.6753299767811,13.4763527474719));
#188327=CARTESIAN_POINT('Ctrl Pts',(16.6871625312223,18.6704719177788,13.4760509755103));
#188328=CARTESIAN_POINT('Ctrl Pts',(16.6915249225735,18.654110051492,13.4750369077715));
#188329=CARTESIAN_POINT('Ctrl Pts',(16.6946904144626,18.6426275115,13.4743290803725));
#188330=CARTESIAN_POINT('Ctrl Pts',(16.7322349721505,18.5107910104225,13.4662399156346));
#188331=CARTESIAN_POINT('Ctrl Pts',(16.7771312058472,18.3936693979983,13.4594083292007));
#188332=CARTESIAN_POINT('Ctrl Pts',(16.9057920733551,18.1305005211885,13.4434861810867));
#188333=CARTESIAN_POINT('Ctrl Pts',(16.9970991709072,17.9891195178236,13.4344327380553));
#188334=CARTESIAN_POINT('Ctrl Pts',(17.1191104020009,17.841923018109,13.4233283528523));
#188335=CARTESIAN_POINT('Ctrl Pts',(17.1343922138713,17.8240987555528,13.4219533516413));
#188336=CARTESIAN_POINT('Ctrl Pts',(17.156353391162,17.7993297660029,13.4199973526351));
#188337=CARTESIAN_POINT('Ctrl Pts',(17.1627888949226,17.7921704363942,13.4194265091625));
#188338=CARTESIAN_POINT('Ctrl Pts',(17.1733018874588,17.7806342495479,13.4184976302671));
#188339=CARTESIAN_POINT('Ctrl Pts',(17.1773495369906,17.7762302925425,13.418140860992));
#188340=CARTESIAN_POINT('Ctrl Pts',(17.1858428974053,17.767067523762,13.4173939949306));
#188341=CARTESIAN_POINT('Ctrl Pts',(17.1902920058684,17.7623119598642,13.4170037547204));
#188342=CARTESIAN_POINT('Ctrl Pts',(17.2008948571889,17.751083087009,13.4160760565232));
#188343=CARTESIAN_POINT('Ctrl Pts',(17.2070677265501,17.7446280825699,13.4155377747377));
#188344=CARTESIAN_POINT('Ctrl Pts',(17.2278430665602,17.7231766182588,13.4137320225775));
#188345=CARTESIAN_POINT('Ctrl Pts',(17.242626711455,17.7083580638623,13.4124566428821));
#188346=CARTESIAN_POINT('Ctrl Pts',(17.323261505804,17.6298951076832,13.405548924508));
#188347=CARTESIAN_POINT('Ctrl Pts',(17.3929621875943,17.5703630572841,13.3997422774234));
#188348=CARTESIAN_POINT('Ctrl Pts',(17.5419202795196,17.4589860863717,13.3876785377884));
#188349=CARTESIAN_POINT('Ctrl Pts',(17.6212465352811,17.4075630532717,13.3814262462463));
#188350=CARTESIAN_POINT('Ctrl Pts',(17.7685848998751,17.3254832848588,13.3702890212522));
#188351=CARTESIAN_POINT('Ctrl Pts',(17.835293607746,17.2927905039487,13.3654068856028));
#188352=CARTESIAN_POINT('Ctrl Pts',(17.9424467989667,17.24709639275,13.3579381768206));
#188353=CARTESIAN_POINT('Ctrl Pts',(17.9817988025074,17.2316900799468,13.355271063532));
#188354=CARTESIAN_POINT('Ctrl Pts',(18.0286043446051,17.2149635577244,13.3522081780424));
#188355=CARTESIAN_POINT('Ctrl Pts',(18.0356335859481,17.2124933412616,13.3517510585795));
#188356=CARTESIAN_POINT('Ctrl Pts',(18.0470291413366,17.2085561798659,13.3510147870947));
#188357=CARTESIAN_POINT('Ctrl Pts',(18.0513873874959,17.2070663095746,13.3507343291401));
#188358=CARTESIAN_POINT('Ctrl Pts',(18.0591363519902,17.2044455323006,13.3502377237466));
#188359=CARTESIAN_POINT('Ctrl Pts',(18.0625251020079,17.2033089786305,13.3500212460875));
#188360=CARTESIAN_POINT('Ctrl Pts',(18.0698013120878,17.2008890922465,13.3495579339211));
#188361=CARTESIAN_POINT('Ctrl Pts',(18.073689609769,17.1996084549,13.3493112588506));
#188362=CARTESIAN_POINT('Ctrl Pts',(18.0843955207839,17.1961167804851,13.3486345154514));
#188363=CARTESIAN_POINT('Ctrl Pts',(18.0912207584813,17.1939290499052,13.3482057979176));
#188364=CARTESIAN_POINT('Ctrl Pts',(18.1280704969853,17.1823234380661,13.3459051140435));
#188365=CARTESIAN_POINT('Ctrl Pts',(18.1582927558532,17.1735406597748,13.3440681093112));
#188366=CARTESIAN_POINT('Ctrl Pts',(18.3467775002746,17.1232951547105,13.3328547375767));
#188367=CARTESIAN_POINT('Ctrl Pts',(18.5092220814565,17.0996165863916,13.3242094004181));
#188368=CARTESIAN_POINT('Ctrl Pts',(18.7898605950997,17.0914986028029,13.3088409057954));
#188369=CARTESIAN_POINT('Ctrl Pts',(18.9069971553275,17.0978333538537,13.3023034437241));
#188370=CARTESIAN_POINT('Ctrl Pts',(19.0371602854161,17.115770382029,13.2946060268684));
#188371=CARTESIAN_POINT('Ctrl Pts',(19.0512998051299,17.1178649997146,13.2937642965802));
#188372=CARTESIAN_POINT('Ctrl Pts',(19.0737683340558,17.1214263640575,13.2924174273655));
#188373=CARTESIAN_POINT('Ctrl Pts',(19.0821117912416,17.122800134449,13.291915231639));
#188374=CARTESIAN_POINT('Ctrl Pts',(19.0968115305499,17.1253110283864,13.2910267433246));
#188375=CARTESIAN_POINT('Ctrl Pts',(19.103171295463,17.126427322881,13.2906411171286));
#188376=CARTESIAN_POINT('Ctrl Pts',(19.1163141434507,17.1287962456996,13.2898416172451));
#188377=CARTESIAN_POINT('Ctrl Pts',(19.1230964028221,17.1300529640896,13.289427617385));
#188378=CARTESIAN_POINT('Ctrl Pts',(19.1404886073149,17.1333636504031,13.2883622544716));
#188379=CARTESIAN_POINT('Ctrl Pts',(19.1510890893745,17.135465737747,13.2877093627331));
#188380=CARTESIAN_POINT('Ctrl Pts',(19.1952560392294,17.1445761124812,13.2849739250263));
#188381=CARTESIAN_POINT('Ctrl Pts',(19.2286642939744,17.1523179369113,13.2828680610068));
#188382=CARTESIAN_POINT('Ctrl Pts',(19.315200780115,17.1745993588527,13.2773137821463));
#188383=CARTESIAN_POINT('Ctrl Pts',(19.3679730893346,17.1904062207996,13.2738269852899));
#188384=CARTESIAN_POINT('Ctrl Pts',(19.5235313423195,17.243694583468,13.263258003926));
#188385=CARTESIAN_POINT('Ctrl Pts',(19.6240876398678,17.2871000885754,13.2560274267358));
#188386=CARTESIAN_POINT('Ctrl Pts',(19.7612323084613,17.3593607083982,13.2457873707386));
#188387=CARTESIAN_POINT('Ctrl Pts',(19.800934003124,17.3819493431767,13.2427764331929));
#188388=CARTESIAN_POINT('Ctrl Pts',(19.8593556375535,17.4177388334853,13.2383012221881));
#188389=CARTESIAN_POINT('Ctrl Pts',(19.8786424606454,17.4299877563269,13.236816294639));
#188390=CARTESIAN_POINT('Ctrl Pts',(19.8983086694723,17.4429290721572,13.2352969564636));
#188391=CARTESIAN_POINT('Ctrl Pts',(19.8988894558718,17.4433116679426,13.2352520823547));
#188392=CARTESIAN_POINT('Ctrl Pts',(19.9087269765776,17.4497991349456,13.2344919136997));
#188393=CARTESIAN_POINT('Ctrl Pts',(19.9179359409109,17.4559764525475,13.2337791349056));
#188394=CARTESIAN_POINT('Ctrl Pts',(19.9604241808332,17.4849639322779,13.2304864497088));
#188395=CARTESIAN_POINT('Ctrl Pts',(19.9930980326395,17.5086517954744,13.2279425500857));
#188396=CARTESIAN_POINT('Ctrl Pts',(20.0309009368652,17.5377424102635,13.2250038123527));
#188397=CARTESIAN_POINT('Ctrl Pts',(20.0367014690806,17.5422543969451,13.2245530206632));
#188398=CARTESIAN_POINT('Ctrl Pts',(20.0460750153494,17.5496243394705,13.2238249282495));
#188399=CARTESIAN_POINT('Ctrl Pts',(20.0496624084111,17.5524637901735,13.2235463673584));
#188400=CARTESIAN_POINT('Ctrl Pts',(20.0560336517982,17.5575403611265,13.2230518458929));
#188401=CARTESIAN_POINT('Ctrl Pts',(20.0588210678533,17.5597729130448,13.222835565615));
#188402=CARTESIAN_POINT('Ctrl Pts',(20.0648072698867,17.5645924155432,13.2223712508755));
#188403=CARTESIAN_POINT('Ctrl Pts',(20.0680041593003,17.567181631879,13.222123383351));
#188404=CARTESIAN_POINT('Ctrl Pts',(20.0768208083879,17.5743650486191,13.2214399969953));
#188405=CARTESIAN_POINT('Ctrl Pts',(20.0824245796626,17.5789789082391,13.2210058733151));
#188406=CARTESIAN_POINT('Ctrl Pts',(20.1132087318636,17.6045918099911,13.2186215980315));
#188407=CARTESIAN_POINT('Ctrl Pts',(20.137923880987,17.62614606254,13.2167094816335));
#188408=CARTESIAN_POINT('Ctrl Pts',(20.2820626923086,17.7578697444379,13.2055013599741));
#188409=CARTESIAN_POINT('Ctrl Pts',(20.388992178696,17.8809254619845,13.1969133998443));
#188410=CARTESIAN_POINT('Ctrl Pts',(20.5467660705564,18.1113624518841,13.1816242300727));
#188411=CARTESIAN_POINT('Ctrl Pts',(20.604640064079,18.2129899499217,13.1751054354326));
#188412=CARTESIAN_POINT('Ctrl Pts',(20.6598598036079,18.3318201577148,13.1674290318761));
#188413=CARTESIAN_POINT('Ctrl Pts',(20.6657499953327,18.3448388609165,13.166587570704));
#188414=CARTESIAN_POINT('Ctrl Pts',(20.6749147243179,18.3656536147415,13.1652410516712));
#188415=CARTESIAN_POINT('Ctrl Pts',(20.6782751894718,18.3734115195486,13.1647389345883));
#188416=CARTESIAN_POINT('Ctrl Pts',(20.6841199576659,18.38712935428,13.1638505378828));
#188417=CARTESIAN_POINT('Ctrl Pts',(20.6866236468956,18.3930809439042,13.1634649242111));
#188418=CARTESIAN_POINT('Ctrl Pts',(20.6917458204163,18.4054145676137,13.1626654036184));
#188419=CARTESIAN_POINT('Ctrl Pts',(20.6943604129559,18.4117981257568,13.1622513702947));
#188420=CARTESIAN_POINT('Ctrl Pts',(20.7009917938761,18.4282170635601,13.1611858229549));
#188421=CARTESIAN_POINT('Ctrl Pts',(20.7049629687823,18.4382705443305,13.1605327792316));
#188422=CARTESIAN_POINT('Ctrl Pts',(20.7212176994973,18.480361843897,13.1577958686475));
#188423=CARTESIAN_POINT('Ctrl Pts',(20.7327978776588,18.5126640291441,13.1556886523177));
#188424=CARTESIAN_POINT('Ctrl Pts',(20.7609219089828,18.5975550055894,13.1501299561792));
#188425=CARTESIAN_POINT('Ctrl Pts',(20.776204957309,18.6505311988173,13.1466400181981));
#188426=CARTESIAN_POINT('Ctrl Pts',(20.8156027094488,18.8102641856276,13.1360650030276));
#188427=CARTESIAN_POINT('Ctrl Pts',(20.8335268487071,18.9183524663537,13.1288315532572));
#188428=CARTESIAN_POINT('Ctrl Pts',(20.8472922902954,19.0764177004891,13.1183507058952));
#188429=CARTESIAN_POINT('Ctrl Pts',(20.8498521887972,19.1256391944558,13.1151025285415));
#188430=CARTESIAN_POINT('Ctrl Pts',(20.8509790979049,19.1917260410636,13.110792261341));
#188431=CARTESIAN_POINT('Ctrl Pts',(20.8510654217678,19.2085489412297,13.1096995107603));
#188432=CARTESIAN_POINT('Ctrl Pts',(20.8505891738575,19.2787017795715,13.1051655061558));
#188433=CARTESIAN_POINT('Ctrl Pts',(20.8482119577541,19.3320045265726,13.1017752562434));
#188434=CARTESIAN_POINT('Ctrl Pts',(20.8431062578115,19.3938546332154,13.0979469027155));
#188435=CARTESIAN_POINT('Ctrl Pts',(20.8423352440206,19.4025398873771,13.0974117488231));
#188436=CARTESIAN_POINT('Ctrl Pts',(20.8410865885957,19.4156831826243,13.0966058557712));
#188437=CARTESIAN_POINT('Ctrl Pts',(20.8406484209221,19.4201447550645,13.0963329802714));
#188438=CARTESIAN_POINT('Ctrl Pts',(20.8398364828793,19.4281506590888,13.0958446087146));
#188439=CARTESIAN_POINT('Ctrl Pts',(20.839467933502,19.4316954529372,13.0956288245853));
#188440=CARTESIAN_POINT('Ctrl Pts',(20.8386476757942,19.4393957802578,13.0951610679864));
#188441=CARTESIAN_POINT('Ctrl Pts',(20.8381926128612,19.4435508983845,13.0949092865756));
#188442=CARTESIAN_POINT('Ctrl Pts',(20.8368798386515,19.4552182478057,13.0942039755402));
#188443=CARTESIAN_POINT('Ctrl Pts',(20.8359941744184,19.4627273584427,13.0937519920002));
#188444=CARTESIAN_POINT('Ctrl Pts',(20.8304597778886,19.5075835447496,13.0910628711354));
#188445=CARTESIAN_POINT('Ctrl Pts',(20.8248557288286,19.5448084995763,13.0888761484958));
#188446=CARTESIAN_POINT('Ctrl Pts',(20.8031483977735,19.6668031566322,13.0818001900211));
#188447=CARTESIAN_POINT('Ctrl Pts',(20.7828560319212,19.7507433865722,13.0770743318795));
#188448=CARTESIAN_POINT('Ctrl Pts',(20.7056113723781,20.0019489289599,13.0627720153405));
#188449=CARTESIAN_POINT('Ctrl Pts',(20.6328342005034,20.1635091290785,13.0532865757092));
#188450=CARTESIAN_POINT('Ctrl Pts',(20.5289143588762,20.3337183705636,13.0416973717006));
#188451=CARTESIAN_POINT('Ctrl Pts',(20.5166570633827,20.353080482869,13.0403548178549));
#188452=CARTESIAN_POINT('Ctrl Pts',(20.4988587372857,20.380210642994,13.0384372474192));
#188453=CARTESIAN_POINT('Ctrl Pts',(20.4935755239224,20.3881464910359,13.0378718467758));
#188454=CARTESIAN_POINT('Ctrl Pts',(20.4849001172674,20.4009888048519,13.0369494253568));
#188455=CARTESIAN_POINT('Ctrl Pts',(20.4815404356815,20.4059171522982,13.0365936357227));
#188456=CARTESIAN_POINT('Ctrl Pts',(20.474460957284,20.4162083858102,13.0358468668041));
#188457=CARTESIAN_POINT('Ctrl Pts',(20.4707371026215,20.4215683921011,13.0354557354522));
#188458=CARTESIAN_POINT('Ctrl Pts',(20.4618130245185,20.4342875176059,13.0345223175787));
#188459=CARTESIAN_POINT('Ctrl Pts',(20.4565905150963,20.4416307780169,13.0339791798033));
#188460=CARTESIAN_POINT('Ctrl Pts',(20.4388081802749,20.4662991574739,13.032140090187));
#188461=CARTESIAN_POINT('Ctrl Pts',(20.4260329179353,20.4834666825315,13.030835824671));
#188462=CARTESIAN_POINT('Ctrl Pts',(20.3548584525755,20.5761442727884,13.0236579371424));
#188463=CARTESIAN_POINT('Ctrl Pts',(20.2916709156374,20.6478222122537,13.0175943698583));
#188464=CARTESIAN_POINT('Ctrl Pts',(20.102757300723,20.8349629094854,13.0003131591558));
#188465=CARTESIAN_POINT('Ctrl Pts',(19.9676031346825,20.9398644550541,12.9888106745707));
#188466=CARTESIAN_POINT('Ctrl Pts',(19.7898897515995,21.0462463434158,12.9755928202219));
#188467=CARTESIAN_POINT('Ctrl Pts',(19.7579566110554,21.0642526920185,12.9732875602183));
#188468=CARTESIAN_POINT('Ctrl Pts',(19.7192673661779,21.0847630859846,12.9705910311118));
#188469=CARTESIAN_POINT('Ctrl Pts',(19.7129478892879,21.0880724329709,12.970153599355));
#188470=CARTESIAN_POINT('Ctrl Pts',(19.7026060929287,21.0934217312935,12.9694428061299));
#188471=CARTESIAN_POINT('Ctrl Pts',(19.6985938287514,21.0954808526779,12.9691682788126));
#188472=CARTESIAN_POINT('Ctrl Pts',(19.6913974003784,21.0991451036556,12.9686781363137));
#188473=CARTESIAN_POINT('Ctrl Pts',(19.6882157445421,21.1007550180335,12.9684622238485));
#188474=CARTESIAN_POINT('Ctrl Pts',(19.6813135643646,21.1042256374955,12.9679955395396));
#188475=CARTESIAN_POINT('Ctrl Pts',(19.6775916307304,21.1060834120953,12.9677449514729));
#188476=CARTESIAN_POINT('Ctrl Pts',(19.6671721546053,21.1112459070399,12.9670463465847));
#188477=CARTESIAN_POINT('Ctrl Pts',(19.6604624883982,21.1145262117225,12.9665998289362));
#188478=CARTESIAN_POINT('Ctrl Pts',(19.6212515661908,21.1334396926026,12.9640090852071));
#188479=CARTESIAN_POINT('Ctrl Pts',(19.588370332991,21.1482767993219,12.9619110771972));
#188480=CARTESIAN_POINT('Ctrl Pts',(19.4811302382674,21.1934051110076,12.9552561063467));
#188481=CARTESIAN_POINT('Ctrl Pts',(19.4054192438977,21.2203112827015,12.9508410842745));
#188482=CARTESIAN_POINT('Ctrl Pts',(19.1504389061178,21.2948981213496,12.9363592389987));
#188483=CARTESIAN_POINT('Ctrl Pts',(18.9664766600931,21.3233449790301,12.9264433370417));
#188484=CARTESIAN_POINT('Ctrl Pts',(18.7590375426672,21.3279676331766,12.9143759547045));
#188485=CARTESIAN_POINT('Ctrl Pts',(18.7369050173621,21.3281136825569,12.9130785724825));
#188486=CARTESIAN_POINT('Ctrl Pts',(18.7063123096548,21.327835849226,12.9112701164498));
#188487=CARTESIAN_POINT('Ctrl Pts',(18.6978503855179,21.3277082517385,12.9107682988479));
#188488=CARTESIAN_POINT('Ctrl Pts',(18.6833118226015,21.327401820025,12.9099032813667));
#188489=CARTESIAN_POINT('Ctrl Pts',(18.677234728488,21.3272475417346,12.9095408536662));
#188490=CARTESIAN_POINT('Ctrl Pts',(18.6647126903276,21.3268756704825,12.9087922693));
#188491=CARTESIAN_POINT('Ctrl Pts',(18.6582679135756,21.326654800264,12.9084060137079));
#188492=CARTESIAN_POINT('Ctrl Pts',(18.6432809836845,21.3260726130555,12.9075054817577));
#188493=CARTESIAN_POINT('Ctrl Pts',(18.6347398547215,21.3256889886289,12.9069905111009));
#188494=CARTESIAN_POINT('Ctrl Pts',(18.6074430812867,21.3242972187698,12.9053389791064));
#188495=CARTESIAN_POINT('Ctrl Pts',(18.5886988360557,21.3230912207108,12.9041962419787));
#188496=CARTESIAN_POINT('Ctrl Pts',(18.4953416648932,21.315836041475,12.8984600578295));
#188497=CARTESIAN_POINT('Ctrl Pts',(18.4210779900157,21.3060823963527,12.8937517313576));
#188498=CARTESIAN_POINT('Ctrl Pts',(18.2404624928557,21.2725431882532,12.8819499532233));
#188499=CARTESIAN_POINT('Ctrl Pts',(18.1351316684906,21.2444435891157,12.8747560833273));
#188500=CARTESIAN_POINT('Ctrl Pts',(17.919239853413,21.1686132225083,12.8596390929953));
#188501=CARTESIAN_POINT('Ctrl Pts',(17.8096130647179,21.1192974322654,12.8517437931516));
#188502=CARTESIAN_POINT('Ctrl Pts',(17.6964404430413,21.0563318112895,12.8437448065828));
#188503=CARTESIAN_POINT('Ctrl Pts',(17.6881662590596,21.0516550795968,12.8431609863434));
#188504=CARTESIAN_POINT('Ctrl Pts',(17.6759498212068,21.0446411361393,12.842300804376));
#188505=CARTESIAN_POINT('Ctrl Pts',(17.6719833410133,21.042346666782,12.842021800709));
#188506=CARTESIAN_POINT('Ctrl Pts',(17.6650378145969,21.0382987699757,12.8415337911044));
#188507=CARTESIAN_POINT('Ctrl Pts',(17.6620555855149,21.0365509090266,12.841324430124));
#188508=CARTESIAN_POINT('Ctrl Pts',(17.655652694039,21.0327771247632,12.840875320619));
#188509=CARTESIAN_POINT('Ctrl Pts',(17.6522334625651,21.0307488737924,12.8406357265764));
#188510=CARTESIAN_POINT('Ctrl Pts',(17.6451818483515,21.0265390344637,12.8401420488052));
#188511=CARTESIAN_POINT('Ctrl Pts',(17.6415502575272,21.0243561464567,12.8398880499292));
#188512=CARTESIAN_POINT('Ctrl Pts',(17.6324230693109,21.0188325770657,12.8392502371787));
#188513=CARTESIAN_POINT('Ctrl Pts',(17.626936053064,21.0154777030106,12.8388673115854));
#188514=CARTESIAN_POINT('Ctrl Pts',(17.6113420138901,21.0058452863295,12.8377802467602));
#188515=CARTESIAN_POINT('Ctrl Pts',(17.6012723391928,20.999507370897,12.8370797383748));
#188516=CARTESIAN_POINT('Ctrl Pts',(17.5675330353624,20.977872387555,12.8347356573142));
#188517=CARTESIAN_POINT('Ctrl Pts',(17.5441146720641,20.962187103051,12.8331137030966));
#188518=CARTESIAN_POINT('Ctrl Pts',(17.3582698101486,20.8322608824912,12.8202242556187));
#188519=CARTESIAN_POINT('Ctrl Pts',(17.2123307147047,20.6961460411557,12.8099003662596));
#188520=CARTESIAN_POINT('Ctrl Pts',(17.0418418322238,20.4851913693457,12.7947367000877));
#188521=CARTESIAN_POINT('Ctrl Pts',(16.9991350587083,20.426403193772,12.7905946435565));
#188522=CARTESIAN_POINT('Ctrl Pts',(16.9524297804521,20.3546198335921,12.7855690505901));
#188523=CARTESIAN_POINT('Ctrl Pts',(16.9454249621493,20.3436332564456,12.7848007971853));
#188524=CARTESIAN_POINT('Ctrl Pts',(16.9341931541268,20.3256528977271,12.7835446515976));
#188525=CARTESIAN_POINT('Ctrl Pts',(16.9299043899144,20.3186979695176,12.7830590448306));
#188526=CARTESIAN_POINT('Ctrl Pts',(16.9223301086203,20.306254364451,12.782190624843));
#188527=CARTESIAN_POINT('Ctrl Pts',(16.9190289863932,20.300775268833,12.78180839016));
#188528=CARTESIAN_POINT('Ctrl Pts',(16.9121165385757,20.289183684089,12.7809999942452));
#188529=CARTESIAN_POINT('Ctrl Pts',(16.9085110338063,20.2830678318283,12.7805736269709));
#188530=CARTESIAN_POINT('Ctrl Pts',(16.8990353467703,20.2668082566338,12.7794404277033));
#188531=CARTESIAN_POINT('Ctrl Pts',(16.8932185809274,20.2566338326202,12.7787316746851));
#188532=CARTESIAN_POINT('Ctrl Pts',(16.8663619662945,20.2087387856,12.7753964933996));
#188533=CARTESIAN_POINT('Ctrl Pts',(16.8463964369092,20.1704304918226,12.7727320466668));
#188534=CARTESIAN_POINT('Ctrl Pts',(16.7969731233895,20.0680778629996,12.7656162602273));
#188535=CARTESIAN_POINT('Ctrl Pts',(16.7695455578597,20.0031840886229,12.7611063920367));
#188536=CARTESIAN_POINT('Ctrl Pts',(16.745419226499,19.9371098451765,12.7565300941239));
#188537=CARTESIAN_POINT('Ctrl Pts',(16.7454193728684,19.937110246035,12.5316746173356));
#188538=CARTESIAN_POINT('Ctrl Pts',(16.7951534513481,20.0733157678728,12.5405908905923));
#188539=CARTESIAN_POINT('Ctrl Pts',(16.8587496331707,20.2040517459169,12.5499845536731));
#188540=CARTESIAN_POINT('Ctrl Pts',(16.9704453902929,20.384042994092,12.5639575310776));
#188541=CARTESIAN_POINT('Ctrl Pts',(17.0083507021618,20.4391243166459,12.5683870471575));
#188542=CARTESIAN_POINT('Ctrl Pts',(17.0853815792362,20.5404358702716,12.5767428575914));
#188543=CARTESIAN_POINT('Ctrl Pts',(17.1240118117388,20.5869656543858,12.5806727923772));
#188544=CARTESIAN_POINT('Ctrl Pts',(17.1848101369709,20.6541244327597,12.5864164111745));
#188545=CARTESIAN_POINT('Ctrl Pts',(17.2055133917509,20.6760345611683,12.588302358832));
#188546=CARTESIAN_POINT('Ctrl Pts',(17.2314460061007,20.70233047705,12.590572768724));
#188547=CARTESIAN_POINT('Ctrl Pts',(17.2362366505817,20.707141720686,12.5909884674441));
#188548=CARTESIAN_POINT('Ctrl Pts',(17.2440063551608,20.7148701142812,12.5916565586287));
#188549=CARTESIAN_POINT('Ctrl Pts',(17.2469709863386,20.7178016111985,12.5919100570225));
#188550=CARTESIAN_POINT('Ctrl Pts',(17.2524865596783,20.7232234076128,12.592379018702));
#188551=CARTESIAN_POINT('Ctrl Pts',(17.2550351084239,20.7257159991752,12.5925946593841));
#188552=CARTESIAN_POINT('Ctrl Pts',(17.2608129353265,20.7313384807468,12.593081184203));
#188553=CARTESIAN_POINT('Ctrl Pts',(17.2640458887809,20.7344645172529,12.5933517675464));
#188554=CARTESIAN_POINT('Ctrl Pts',(17.2736234849937,20.7436665014956,12.5941486019655));
#188555=CARTESIAN_POINT('Ctrl Pts',(17.279996102778,20.7497133726914,12.5946726503172));
#188556=CARTESIAN_POINT('Ctrl Pts',(17.3265472395098,20.793337530867,12.5984580705629));
#188557=CARTESIAN_POINT('Ctrl Pts',(17.3681429756252,20.8293791371839,12.6016115533307));
#188558=CARTESIAN_POINT('Ctrl Pts',(17.4341018510134,20.8821738108328,12.6063563622713));
#188559=CARTESIAN_POINT('Ctrl Pts',(17.457486914923,20.9001037707016,12.6079923190341));
#188560=CARTESIAN_POINT('Ctrl Pts',(17.5992267863209,21.004154141963,12.6176841330977));
#188561=CARTESIAN_POINT('Ctrl Pts',(17.7258770430646,21.0782979248174,12.6254620917527));
#188562=CARTESIAN_POINT('Ctrl Pts',(17.9081626770306,21.1610197036013,12.6366045313939));
#188563=CARTESIAN_POINT('Ctrl Pts',(17.9579868512715,21.1813774040388,12.6396414866404));
#188564=CARTESIAN_POINT('Ctrl Pts',(18.0400744225546,21.2113209118695,12.6446710844814));
#188565=CARTESIAN_POINT('Ctrl Pts',(18.0718868047725,21.2220749338643,12.6466262603229));
#188566=CARTESIAN_POINT('Ctrl Pts',(18.1142573081268,21.2352837702599,12.6492437388411));
#188567=CARTESIAN_POINT('Ctrl Pts',(18.1245987111298,21.2384209847085,12.6498836208925));
#188568=CARTESIAN_POINT('Ctrl Pts',(18.141579338128,21.2434306477105,12.650936175322));
#188569=CARTESIAN_POINT('Ctrl Pts',(18.14820457672,21.2453500924617,12.6513473072914));
#188570=CARTESIAN_POINT('Ctrl Pts',(18.161049705212,21.2490035948981,12.6521453601056));
#188571=CARTESIAN_POINT('Ctrl Pts',(18.1672683877396,21.2507416432841,12.6525321457706));
#188572=CARTESIAN_POINT('Ctrl Pts',(18.1816489827792,21.2546900096582,12.6534276069409));
#188573=CARTESIAN_POINT('Ctrl Pts',(18.1898163403436,21.2568799190382,12.6539369389564));
#188574=CARTESIAN_POINT('Ctrl Pts',(18.2118246926749,21.2626398964955,12.6553115652768));
#188575=CARTESIAN_POINT('Ctrl Pts',(18.2256889025591,21.2661187627386,12.6561797897569));
#188576=CARTESIAN_POINT('Ctrl Pts',(18.3535020627039,21.2968177226203,12.6642060517678));
#188577=CARTESIAN_POINT('Ctrl Pts',(18.4694728363121,21.3146710214679,12.6716675300691));
#188578=CARTESIAN_POINT('Ctrl Pts',(18.7496195305198,21.3342630297295,12.69001330445));
#188579=CARTESIAN_POINT('Ctrl Pts',(18.9136997210596,21.3267027436058,12.7010402575659));
#188580=CARTESIAN_POINT('Ctrl Pts',(19.1062175737581,21.2952568099131,12.7134218699726));
#188581=CARTESIAN_POINT('Ctrl Pts',(19.1370520153354,21.289514298128,12.7153857117907));
#188582=CARTESIAN_POINT('Ctrl Pts',(19.1747568655624,21.2816215596416,12.7177541337578));
#188583=CARTESIAN_POINT('Ctrl Pts',(19.1817570641724,21.2801191054776,12.7181924416916));
#188584=CARTESIAN_POINT('Ctrl Pts',(19.1927461194891,21.277702141699,12.7188781454743));
#188585=CARTESIAN_POINT('Ctrl Pts',(19.1967401009818,21.2768115461601,12.7191268737939));
#188586=CARTESIAN_POINT('Ctrl Pts',(19.2042181176983,21.2751212898615,12.7195916193548));
#188587=CARTESIAN_POINT('Ctrl Pts',(19.2077026699488,21.2743243947982,12.7198077854625));
#188588=CARTESIAN_POINT('Ctrl Pts',(19.2156751146127,21.272479886332,12.7203014790328));
#188589=CARTESIAN_POINT('Ctrl Pts',(19.2201616077601,21.2714264436882,12.720578668207));
#188590=CARTESIAN_POINT('Ctrl Pts',(19.2319008280872,21.2686295599241,12.7213023690986));
#188591=CARTESIAN_POINT('Ctrl Pts',(19.2391479157896,21.2668624047758,12.72174755272));
#188592=CARTESIAN_POINT('Ctrl Pts',(19.2875407330671,21.2547907899921,12.7247105966769));
#188593=CARTESIAN_POINT('Ctrl Pts',(19.3283811712733,21.2432892767676,12.7271643235586));
#188594=CARTESIAN_POINT('Ctrl Pts',(19.3779669887142,21.2277019668476,12.7301163733928));
#188595=CARTESIAN_POINT('Ctrl Pts',(19.3870632233857,21.224774748226,12.7306567747096));
#188596=CARTESIAN_POINT('Ctrl Pts',(19.4096895645133,21.2173240335051,12.7319988559527));
#188597=CARTESIAN_POINT('Ctrl Pts',(19.4231944651367,21.2127251353947,12.7327979870546));
#188598=CARTESIAN_POINT('Ctrl Pts',(19.5716113515952,21.1605038266174,12.7415693435315));
#188599=CARTESIAN_POINT('Ctrl Pts',(19.7014134825564,21.0994578283077,12.7491651043511));
#188600=CARTESIAN_POINT('Ctrl Pts',(19.9037846689524,20.9779011817902,12.7621659333495));
#188601=CARTESIAN_POINT('Ctrl Pts',(19.980248981247,20.9248251189157,12.7673867183288));
#188602=CARTESIAN_POINT('Ctrl Pts',(20.0694784653254,20.8537512284259,12.7740313484491));
#188603=CARTESIAN_POINT('Ctrl Pts',(20.0857869476221,20.8403576435688,12.77526985305));
#188604=CARTESIAN_POINT('Ctrl Pts',(20.1087310760519,20.8209328447991,12.7770483114854));
#188605=CARTESIAN_POINT('Ctrl Pts',(20.115533178869,20.8150995505733,12.7775801750663));
#188606=CARTESIAN_POINT('Ctrl Pts',(20.1272183777149,20.8049491932252,12.7785019707523));
#188607=CARTESIAN_POINT('Ctrl Pts',(20.1321189842717,20.8006524094719,12.7788910586014));
#188608=CARTESIAN_POINT('Ctrl Pts',(20.1414741740665,20.7923731854999,12.7796386720994));
#188609=CARTESIAN_POINT('Ctrl Pts',(20.1459318977554,20.7883943760029,12.7799970434757));
#188610=CARTESIAN_POINT('Ctrl Pts',(20.1575015097735,20.7779794046365,12.7809327851854));
#188611=CARTESIAN_POINT('Ctrl Pts',(20.1645865470585,20.7715137389722,12.7815114001816));
#188612=CARTESIAN_POINT('Ctrl Pts',(20.1887074057308,20.7491991958307,12.7835007012245));
#188613=CARTESIAN_POINT('Ctrl Pts',(20.2055252726324,20.7331181644514,12.7849212977454));
#188614=CARTESIAN_POINT('Ctrl Pts',(20.3440308911561,20.5962396930944,12.7969104829135));
#188615=CARTESIAN_POINT('Ctrl Pts',(20.4508717111137,20.4613671797419,12.8081468609156));
#188616=CARTESIAN_POINT('Ctrl Pts',(20.5871336332421,20.2384532413753,12.8254112865684));
#188617=CARTESIAN_POINT('Ctrl Pts',(20.6290755032049,20.1588687930003,12.8313409597301));
#188618=CARTESIAN_POINT('Ctrl Pts',(20.6815952813217,20.0416904362553,12.8395443291328));
#188619=CARTESIAN_POINT('Ctrl Pts',(20.6963944125211,20.0060991021721,12.8419694562089));
#188620=CARTESIAN_POINT('Ctrl Pts',(20.712944117017,19.9630153746079,12.8448097518762));
#188621=CARTESIAN_POINT('Ctrl Pts',(20.7156353429459,19.9558948338867,12.8452760977527));
#188622=CARTESIAN_POINT('Ctrl Pts',(20.7197486755566,19.9448315622699,12.8459957324565));
#188623=CARTESIAN_POINT('Ctrl Pts',(20.7211975471602,19.9408989474726,12.8462505756605));
#188624=CARTESIAN_POINT('Ctrl Pts',(20.7238565774959,19.9336150400623,12.8467207777181));
#188625=CARTESIAN_POINT('Ctrl Pts',(20.7250699440785,19.9302650229383,12.8469363218853));
#188626=CARTESIAN_POINT('Ctrl Pts',(20.7277860805794,19.9227064243602,12.8474210607724));
#188627=CARTESIAN_POINT('Ctrl Pts',(20.7292839814788,19.9184961510029,12.8476899642741));
#188628=CARTESIAN_POINT('Ctrl Pts',(20.7336431805049,19.9061194338257,12.8484772926983));
#188629=CARTESIAN_POINT('Ctrl Pts',(20.7364677935121,19.897940039864,12.848993592581));
#188630=CARTESIAN_POINT('Ctrl Pts',(20.7558510235146,19.8406752894476,12.8525817279561));
#188631=CARTESIAN_POINT('Ctrl Pts',(20.7706546720376,19.7910096722866,12.8555580212388));
#188632=CARTESIAN_POINT('Ctrl Pts',(20.7889977551949,19.720052572512,12.8596850524636));
#188633=CARTESIAN_POINT('Ctrl Pts',(20.794056626284,19.6991772580519,12.8608841341525));
#188634=CARTESIAN_POINT('Ctrl Pts',(20.8292168714097,19.5437954003393,12.8697211243266));
#188635=CARTESIAN_POINT('Ctrl Pts',(20.8464361376554,19.4067109023162,12.8770516832755));
#188636=CARTESIAN_POINT('Ctrl Pts',(20.8526909257654,19.178186584094,12.8896554780303));
#188637=CARTESIAN_POINT('Ctrl Pts',(20.8493361875485,19.0873956436999,12.8947578895238));
#188638=CARTESIAN_POINT('Ctrl Pts',(20.838061943456,18.9763804482943,12.9012593026213));
#188639=CARTESIAN_POINT('Ctrl Pts',(20.8356513394552,18.9556872552153,12.90248217698));
#188640=CARTESIAN_POINT('Ctrl Pts',(20.8317737292689,18.9261950672429,12.9042420623618));
#188641=CARTESIAN_POINT('Ctrl Pts',(20.8305558525056,18.917364132717,12.9047712157949));
#188642=CARTESIAN_POINT('Ctrl Pts',(20.8283522576459,18.9020987344584,12.9056898112319));
#188643=CARTESIAN_POINT('Ctrl Pts',(20.8273925642964,18.8956605935684,12.9060784249497));
#188644=CARTESIAN_POINT('Ctrl Pts',(20.8254934730554,18.8833113130543,12.9068261833565));
#188645=CARTESIAN_POINT('Ctrl Pts',(20.8245586678411,18.8773995225478,12.907185178844));
#188646=CARTESIAN_POINT('Ctrl Pts',(20.8220516906762,18.8619696246711,12.9081248994816));
#188647=CARTESIAN_POINT('Ctrl Pts',(20.8204395191019,18.8524582393242,12.9087068901558));
#188648=CARTESIAN_POINT('Ctrl Pts',(20.8146595297657,18.8197176411792,12.9107198241736));
#188649=CARTESIAN_POINT('Ctrl Pts',(20.8101684429913,18.7965479657116,12.9121609969831));
#188650=CARTESIAN_POINT('Ctrl Pts',(20.7711441855071,18.6118096603558,12.9237898296514));
#188651=CARTESIAN_POINT('Ctrl Pts',(20.7181976114173,18.4547423596878,12.9345920158262));
#188652=CARTESIAN_POINT('Ctrl Pts',(20.5930494831104,18.1902849276127,12.9539265501128));
#188653=CARTESIAN_POINT('Ctrl Pts',(20.5282543893181,18.0802559244732,12.9623538704573));
#188654=CARTESIAN_POINT('Ctrl Pts',(20.4469595082992,17.9669732798619,12.9710015854889));
#188655=CARTESIAN_POINT('Ctrl Pts',(20.4398861629441,17.9572914326574,12.9717402882779));
#188656=CARTESIAN_POINT('Ctrl Pts',(20.4297252028044,17.9436285458154,12.9727815710676));
#188657=CARTESIAN_POINT('Ctrl Pts',(20.4267051999686,17.9395978317186,12.9730886162176));
#188658=CARTESIAN_POINT('Ctrl Pts',(20.4214803084455,17.9326759298843,12.9736155942289));
#188659=CARTESIAN_POINT('Ctrl Pts',(20.4192823126398,17.9297795868355,12.9738360046449));
#188660=CARTESIAN_POINT('Ctrl Pts',(20.4150096327264,17.9241794106607,12.9742619733937));
#188661=CARTESIAN_POINT('Ctrl Pts',(20.4129358814965,17.9214749243734,12.9744675969283));
#188662=CARTESIAN_POINT('Ctrl Pts',(20.4073307637021,17.9142014415955,12.9750203988233));
#188663=CARTESIAN_POINT('Ctrl Pts',(20.403787188729,17.9096418279478,12.9753667215354));
#188664=CARTESIAN_POINT('Ctrl Pts',(20.3906100440894,17.8928288775598,12.9766431644192));
#188665=CARTESIAN_POINT('Ctrl Pts',(20.3808596249719,17.8806672018744,12.9775653464204));
#188666=CARTESIAN_POINT('Ctrl Pts',(20.2843015067537,17.7629192057729,12.9864949173469));
#188667=CARTESIAN_POINT('Ctrl Pts',(20.1875820394311,17.6658519887214,12.9938782343677));
#188668=CARTESIAN_POINT('Ctrl Pts',(19.9630236887574,17.4803733886287,13.0096948238436));
#188669=CARTESIAN_POINT('Ctrl Pts',(19.8334828130662,17.3953189210896,13.018114330301));
#188670=CARTESIAN_POINT('Ctrl Pts',(19.6768994534707,17.3154573245388,13.0283508688474));
#188671=CARTESIAN_POINT('Ctrl Pts',(19.6578075301877,17.3060797884219,13.0295990397689));
#188672=CARTESIAN_POINT('Ctrl Pts',(19.6304507546339,17.2931507225657,13.0313889745371));
#188673=CARTESIAN_POINT('Ctrl Pts',(19.6222991765023,17.2893615387726,13.0319225025498));
#188674=CARTESIAN_POINT('Ctrl Pts',(19.6081915341316,17.2829126816721,13.0328462669579));
#188675=CARTESIAN_POINT('Ctrl Pts',(19.6022468120009,17.2802283880722,13.033235649259));
#188676=CARTESIAN_POINT('Ctrl Pts',(19.5908383093738,17.2751403093181,13.0339831876487));
#188677=CARTESIAN_POINT('Ctrl Pts',(19.5853765737099,17.2727320724365,13.0343411863817));
#188678=CARTESIAN_POINT('Ctrl Pts',(19.5711423553406,17.266527566471,13.0352745420045));
#188679=CARTESIAN_POINT('Ctrl Pts',(19.5623542888184,17.2627675869218,13.0358511310905));
#188680=CARTESIAN_POINT('Ctrl Pts',(19.5322726147958,17.2501374535425,13.0378261508669));
#188681=CARTESIAN_POINT('Ctrl Pts',(19.5108602227467,17.241556113546,13.0392343011635));
#188682=CARTESIAN_POINT('Ctrl Pts',(19.3263063261939,17.17107133474,13.0513951056558));
#188683=CARTESIAN_POINT('Ctrl Pts',(19.156257656654,17.129219233369,13.0628424179537));
#188684=CARTESIAN_POINT('Ctrl Pts',(18.8959417329819,17.098381408126,13.0801628140937));
#188685=CARTESIAN_POINT('Ctrl Pts',(18.8082757903396,17.0934855416282,13.0859453020997));
#188686=CARTESIAN_POINT('Ctrl Pts',(18.6825553971514,17.0942840469478,13.0939733679116));
#188687=CARTESIAN_POINT('Ctrl Pts',(18.644567080935,17.0955484781117,13.0963639277373));
#188688=CARTESIAN_POINT('Ctrl Pts',(18.5990627520819,17.0982912120156,13.0991692106039));
#188689=CARTESIAN_POINT('Ctrl Pts',(18.591497059115,17.0987880315803,13.0996336871323));
#188690=CARTESIAN_POINT('Ctrl Pts',(18.5797601617785,17.0996221129831,13.1003510636406));
#188691=CARTESIAN_POINT('Ctrl Pts',(18.575587102031,17.0999311086715,13.100605502753));
#188692=CARTESIAN_POINT('Ctrl Pts',(18.5678619244165,17.1005261577805,13.1010753299295));
#188693=CARTESIAN_POINT('Ctrl Pts',(18.5643096431425,17.1008088044108,13.1012909009335));
#188694=CARTESIAN_POINT('Ctrl Pts',(18.5562959071319,17.1014668052009,13.1017761666201));
#188695=CARTESIAN_POINT('Ctrl Pts',(18.5518349322367,17.1018473422924,13.1020455672483));
#188696=CARTESIAN_POINT('Ctrl Pts',(18.5387170283978,17.1030082753438,13.1028357033986));
#188697=CARTESIAN_POINT('Ctrl Pts',(18.5300635387925,17.1038278485444,13.1033542910794));
#188698=CARTESIAN_POINT('Ctrl Pts',(18.4689434379666,17.1099965853368,13.1069999693863));
#188699=CARTESIAN_POINT('Ctrl Pts',(18.4166831346991,17.1172518477538,13.1100279943347));
#188700=CARTESIAN_POINT('Ctrl Pts',(18.3491993977167,17.1292058904386,13.1138841981394));
#188701=CARTESIAN_POINT('Ctrl Pts',(18.3336857616449,17.1321333024201,13.114766939039));
#188702=CARTESIAN_POINT('Ctrl Pts',(18.268355443228,17.145219532284,13.1184736985784));
#188703=CARTESIAN_POINT('Ctrl Pts',(18.2188789771997,17.1569979372192,13.1212551283587));
#188704=CARTESIAN_POINT('Ctrl Pts',(18.0644203227247,17.1997013293051,13.1299802793178));
#188705=CARTESIAN_POINT('Ctrl Pts',(17.961387342354,17.2369868056763,13.1358712586438));
#188706=CARTESIAN_POINT('Ctrl Pts',(17.8114224953119,17.304803598809,13.145022312314));
#188707=CARTESIAN_POINT('Ctrl Pts',(17.762054610024,17.329496483267,13.1481336795467));
#188708=CARTESIAN_POINT('Ctrl Pts',(17.6836215171005,17.3726384286187,13.1532834962776));
#188709=CARTESIAN_POINT('Ctrl Pts',(17.6539415161595,17.3899174376698,13.1552824414187));
#188710=CARTESIAN_POINT('Ctrl Pts',(17.6154867425232,17.4135757302737,13.1579451847157));
#188711=CARTESIAN_POINT('Ctrl Pts',(17.6063211065328,17.4193119079438,13.1585854071978));
#188712=CARTESIAN_POINT('Ctrl Pts',(17.5913800203159,17.4288226300313,13.1596383789554));
#188713=CARTESIAN_POINT('Ctrl Pts',(17.5855782965406,17.4325556839493,13.1600495854226));
#188714=CARTESIAN_POINT('Ctrl Pts',(17.5743824820032,17.4398371338546,13.1608476809128));
#188715=CARTESIAN_POINT('Ctrl Pts',(17.5689861673034,17.4433819828225,13.1612344342161));
#188716=CARTESIAN_POINT('Ctrl Pts',(17.5565627299155,17.4516245643296,13.1621296719968));
#188717=CARTESIAN_POINT('Ctrl Pts',(17.5495473935053,17.4563397854982,13.1626388119543));
#188718=CARTESIAN_POINT('Ctrl Pts',(17.5307542285844,17.4691353037707,13.164012583961));
#188719=CARTESIAN_POINT('Ctrl Pts',(17.5190297831873,17.4772928843191,13.1648801405224));
#188720=CARTESIAN_POINT('Ctrl Pts',(17.3924219185643,17.5672985341675,13.1743651190266));
#188721=CARTESIAN_POINT('Ctrl Pts',(17.2859326065109,17.6602989546083,13.1834322370289));
#188722=CARTESIAN_POINT('Ctrl Pts',(17.1234053906142,17.8336792176033,13.1990666174563));
#188723=CARTESIAN_POINT('Ctrl Pts',(17.062220711904,17.9086245762899,13.2054947896265));
#188724=CARTESIAN_POINT('Ctrl Pts',(16.968666055254,18.0407261198294,13.2160579281447));
#188725=CARTESIAN_POINT('Ctrl Pts',(16.9334396892371,18.0956843074626,13.2202520518305));
#188726=CARTESIAN_POINT('Ctrl Pts',(16.8942250343322,18.1635792794386,13.225123492732));
#188727=CARTESIAN_POINT('Ctrl Pts',(16.8877510527217,18.1750333331444,13.2259350812737));
#188728=CARTESIAN_POINT('Ctrl Pts',(16.8788540500822,18.1911226352675,13.2270600795359));
#188729=CARTESIAN_POINT('Ctrl Pts',(16.8763409370769,18.1957073614607,13.2273789641767));
#188730=CARTESIAN_POINT('Ctrl Pts',(16.8720920943216,18.2035272070418,13.2279199320434));
#188731=CARTESIAN_POINT('Ctrl Pts',(16.8703477570075,18.2067576011281,13.2281425593833));
#188732=CARTESIAN_POINT('Ctrl Pts',(16.867022326838,18.212954576243,13.2285679887888));
#188733=CARTESIAN_POINT('Ctrl Pts',(16.865439891317,18.215920394857,13.2287708789558));
#188734=CARTESIAN_POINT('Ctrl Pts',(16.8612708347414,18.2237791006438,13.229306628299));
#188735=CARTESIAN_POINT('Ctrl Pts',(16.8586963046326,18.2286784221811,13.2296387248677));
#188736=CARTESIAN_POINT('Ctrl Pts',(16.8496512072843,18.2460563702032,13.2308101504289));
#188737=CARTESIAN_POINT('Ctrl Pts',(16.8432855781046,18.2585895948662,13.2316431345393));
#188738=CARTESIAN_POINT('Ctrl Pts',(16.7641645776927,18.418290257541,13.242119199025));
#188739=CARTESIAN_POINT('Ctrl Pts',(16.70863132133,18.5733961322497,13.2508474035975));
#188740=CARTESIAN_POINT('Ctrl Pts',(16.6409703157188,18.8655650534694,13.2671776861255));
#188741=CARTESIAN_POINT('Ctrl Pts',(16.6231411421165,19.0003664244169,13.2746743969852));
#188742=CARTESIAN_POINT('Ctrl Pts',(16.6177334382085,19.152784649311,13.2835989613812));
#188743=CARTESIAN_POINT('Ctrl Pts',(16.6173369766561,19.1696380758585,13.2845914629408));
#188744=CARTESIAN_POINT('Ctrl Pts',(16.6170471058789,19.1946775550146,13.286075152639));
#188745=CARTESIAN_POINT('Ctrl Pts',(16.6169998255318,19.2028614149966,13.2865615231206));
#188746=CARTESIAN_POINT('Ctrl Pts',(16.6170001372642,19.2174435235817,13.2874307960698));
#188747=CARTESIAN_POINT('Ctrl Pts',(16.6170292805232,19.2238417019445,13.2878131157006));
#188748=CARTESIAN_POINT('Ctrl Pts',(16.6171518843233,19.2373316694133,13.2886211592693));
#188749=CARTESIAN_POINT('Ctrl Pts',(16.6172519794773,19.2444233057235,13.2890470865517));
#188750=CARTESIAN_POINT('Ctrl Pts',(16.6176113756265,19.2631994775609,13.2901778764416));
#188751=CARTESIAN_POINT('Ctrl Pts',(16.6179318027065,19.2748824753308,13.2908846455564));
#188752=CARTESIAN_POINT('Ctrl Pts',(16.6198779960648,19.3293736722594,13.2941962897627));
#188753=CARTESIAN_POINT('Ctrl Pts',(16.6227060715008,19.3721263554048,13.2968385334104));
#188754=CARTESIAN_POINT('Ctrl Pts',(16.6340979511182,19.4899338765473,13.3042463177318));
#188755=CARTESIAN_POINT('Ctrl Pts',(16.6453836996307,19.5646562235029,13.309090131725));
#188756=CARTESIAN_POINT('Ctrl Pts',(16.6815642385049,19.7400858193889,13.3207652590004));
#188757=CARTESIAN_POINT('Ctrl Pts',(16.7099064195447,19.8398517871678,13.3276519356594));
#188758=CARTESIAN_POINT('Ctrl Pts',(16.7454193976962,19.9371103140301,13.3344632337298));
#188759=CARTESIAN_POINT('Origin',(18.734,19.211,0.));
#188760=CARTESIAN_POINT('',(16.7430900140495,19.9379407811485,14.3554399645868));
#188761=CARTESIAN_POINT('',(16.7454193878426,19.9371102870445,14.1348940376456));
#188762=CARTESIAN_POINT('',(16.7454193623258,19.9371102171621,0.));
#188763=CARTESIAN_POINT('',(16.6201365181454,19.2114595403695,14.3110918013087));
#188764=CARTESIAN_POINT('Ctrl Pts',(16.6203928462353,19.2114685807018,14.3109441064946));
#188765=CARTESIAN_POINT('Ctrl Pts',(16.6199115541233,19.4590066736441,14.325776059192));
#188766=CARTESIAN_POINT('Ctrl Pts',(16.6606018319505,19.7063940375655,14.3406080118894));
#188767=CARTESIAN_POINT('Ctrl Pts',(16.7430900140495,19.9379407811485,14.3554399645868));
#188768=CARTESIAN_POINT('Ctrl Pts',(16.6170000287543,19.2113489207865,14.3128990289819));
#188769=CARTESIAN_POINT('Ctrl Pts',(16.6169985638862,19.2024611564085,14.3123784634678));
#188770=CARTESIAN_POINT('Ctrl Pts',(16.6170530690492,19.1935735507239,14.3118562095885));
#188771=CARTESIAN_POINT('Ctrl Pts',(16.6172707415281,19.176062414464,14.3108237389372));
#188772=CARTESIAN_POINT('Ctrl Pts',(16.6174306466518,19.1674390346876,14.3103136339808));
#188773=CARTESIAN_POINT('Ctrl Pts',(16.6177963852388,19.1526059883968,14.30943324476));
#188774=CARTESIAN_POINT('Ctrl Pts',(16.617976868931,19.1463957645254,14.3090637552432));
#188775=CARTESIAN_POINT('Ctrl Pts',(16.6183911392897,19.1340179091227,14.3083254924661));
#188776=CARTESIAN_POINT('Ctrl Pts',(16.6186245665655,19.1278503264735,14.3079567340467));
#188777=CARTESIAN_POINT('Ctrl Pts',(16.6191442765127,19.1155429556841,14.3072190479821));
#188778=CARTESIAN_POINT('Ctrl Pts',(16.6194303342871,19.1094032181427,14.3068501309369));
#188779=CARTESIAN_POINT('Ctrl Pts',(16.6202771219087,19.0927853661848,14.3058491121201));
#188780=CARTESIAN_POINT('Ctrl Pts',(16.6208890191119,19.0823101353717,14.3052154108766));
#188781=CARTESIAN_POINT('Ctrl Pts',(16.6234852744379,19.0428994846476,14.3028208456677));
#188782=CARTESIAN_POINT('Ctrl Pts',(16.6259862442916,19.0140023736038,14.3010438784631));
#188783=CARTESIAN_POINT('Ctrl Pts',(16.6533446372121,18.7590033753178,14.2851680809543));
#188784=CARTESIAN_POINT('Ctrl Pts',(16.7139033612549,18.5382508517552,14.2698309810564));
#188785=CARTESIAN_POINT('Ctrl Pts',(16.8323264863085,18.2789845503511,14.251309568682));
#188786=CARTESIAN_POINT('Ctrl Pts',(16.858423151156,18.2275226793277,14.2476192267588));
#188787=CARTESIAN_POINT('Ctrl Pts',(16.892613336978,18.1664253358584,14.2432746839185));
#188788=CARTESIAN_POINT('Ctrl Pts',(16.8987294823071,18.1557165237836,14.2425146347496));
#188789=CARTESIAN_POINT('Ctrl Pts',(16.9075039228619,18.1406603206734,14.2414487404887));
#188790=CARTESIAN_POINT('Ctrl Pts',(16.9100847347766,18.136268379794,14.2411381445089));
#188791=CARTESIAN_POINT('Ctrl Pts',(16.9145399633951,18.1287488880544,14.240606992286));
#188792=CARTESIAN_POINT('Ctrl Pts',(16.9164066454085,18.1256167993642,14.2403859386258));
#188793=CARTESIAN_POINT('Ctrl Pts',(16.9200260111282,18.1195794212297,14.239960220242));
#188794=CARTESIAN_POINT('Ctrl Pts',(16.9217775888977,18.1166735198579,14.23975548322));
#188795=CARTESIAN_POINT('Ctrl Pts',(16.9264891216629,18.1088993304523,14.2392081669173));
#188796=CARTESIAN_POINT('Ctrl Pts',(16.9294617805855,18.1040387190568,14.2388664129858));
#188797=CARTESIAN_POINT('Ctrl Pts',(16.9403739741107,18.0863569031671,14.2376245782977));
#188798=CARTESIAN_POINT('Ctrl Pts',(16.948431034944,18.0736082838159,14.2367318891418));
#188799=CARTESIAN_POINT('Ctrl Pts',(17.041094420383,17.9303995724018,14.2267216463254));
#188800=CARTESIAN_POINT('Ctrl Pts',(17.1397034617471,17.8095366123898,14.2184157408545));
#188801=CARTESIAN_POINT('Ctrl Pts',(17.3440926802485,17.6088174435505,14.2028364393363));
#188802=CARTESIAN_POINT('Ctrl Pts',(17.4458049400079,17.5259542609323,14.1956400440395));
#188803=CARTESIAN_POINT('Ctrl Pts',(17.5686447156221,17.4435369253067,14.1870590286926));
#188804=CARTESIAN_POINT('Ctrl Pts',(17.5828913248143,17.4342255481382,14.1860657803944));
#188805=CARTESIAN_POINT('Ctrl Pts',(17.6055781914815,17.4197851274794,14.1844863127889));
#188806=CARTESIAN_POINT('Ctrl Pts',(17.6139449052986,17.4145415180481,14.1839042903245));
#188807=CARTESIAN_POINT('Ctrl Pts',(17.6282406453183,17.4057207434189,14.1829104659138));
#188808=CARTESIAN_POINT('Ctrl Pts',(17.634151148038,17.4021137554247,14.1824997600373));
#188809=CARTESIAN_POINT('Ctrl Pts',(17.6458191978139,17.3950714519545,14.1816892866909));
#188810=CARTESIAN_POINT('Ctrl Pts',(17.6515755820502,17.3916343611884,14.1812895902028));
#188811=CARTESIAN_POINT('Ctrl Pts',(17.6627560757811,17.3850304208536,14.1805135085188));
#188812=CARTESIAN_POINT('Ctrl Pts',(17.6681781487294,17.3818602488658,14.1801372496098));
#188813=CARTESIAN_POINT('Ctrl Pts',(17.6809345058232,17.3744778522702,14.1792522492826));
#188814=CARTESIAN_POINT('Ctrl Pts',(17.6882800451251,17.3702853814724,14.1787428005507));
#188815=CARTESIAN_POINT('Ctrl Pts',(17.7081126415037,17.3591229434267,14.1773676551297));
#188816=CARTESIAN_POINT('Ctrl Pts',(17.7206453590406,17.3522353939029,14.1764990248226));
#188817=CARTESIAN_POINT('Ctrl Pts',(17.8361885670301,17.2902526914411,14.1684928198603));
#188818=CARTESIAN_POINT('Ctrl Pts',(17.9435076071107,17.2436541817485,14.1610536420035));
#188819=CARTESIAN_POINT('Ctrl Pts',(18.2081745450131,17.1538992397477,14.1427987640214));
#188820=CARTESIAN_POINT('Ctrl Pts',(18.3677477054533,17.1195853421646,14.1318430299218));
#188821=CARTESIAN_POINT('Ctrl Pts',(18.5620752498504,17.1007415976985,14.1194365949179));
#188822=CARTESIAN_POINT('Ctrl Pts',(18.5945457282129,17.0983473025879,14.1173963057822));
#188823=CARTESIAN_POINT('Ctrl Pts',(18.6342938831879,17.0963368716928,14.1149489412328));
#188824=CARTESIAN_POINT('Ctrl Pts',(18.6415292356707,17.0960081283399,14.1145054801349));
#188825=CARTESIAN_POINT('Ctrl Pts',(18.6528732572232,17.0955510295723,14.1138135308002));
#188826=CARTESIAN_POINT('Ctrl Pts',(18.6569807760099,17.0953975007868,14.1135636703893));
#188827=CARTESIAN_POINT('Ctrl Pts',(18.6646584272161,17.0951329191159,14.1130979523566));
#188828=CARTESIAN_POINT('Ctrl Pts',(18.6682283542751,17.095018939467,14.1128819390276));
#188829=CARTESIAN_POINT('Ctrl Pts',(18.6763769916468,17.0947794140561,14.1123900749896));
#188830=CARTESIAN_POINT('Ctrl Pts',(18.6809558226973,17.0946596928605,14.1121145531211));
#188831=CARTESIAN_POINT('Ctrl Pts',(18.6950269312929,17.0943374754427,14.1112704070589));
#188832=CARTESIAN_POINT('Ctrl Pts',(18.7045203619703,17.0941839707978,14.1107044537608));
#188833=CARTESIAN_POINT('Ctrl Pts',(18.8345138804642,17.0929567271269,14.1029998535792));
#188834=CARTESIAN_POINT('Ctrl Pts',(18.9549089011955,17.1021097502756,14.0963869136496));
#188835=CARTESIAN_POINT('Ctrl Pts',(19.1811224308796,17.138905726983,14.0839139817551));
#188836=CARTESIAN_POINT('Ctrl Pts',(19.2868566443039,17.1645783150994,14.0780602696622));
#188837=CARTESIAN_POINT('Ctrl Pts',(19.4610751541079,17.2213729371848,14.0678643344856));
#188838=CARTESIAN_POINT('Ctrl Pts',(19.5307231228407,17.248225250884,14.0636328979163));
#188839=CARTESIAN_POINT('Ctrl Pts',(19.6159165864917,17.2863536376601,14.058182703268));
#188840=CARTESIAN_POINT('Ctrl Pts',(19.6329259778691,17.2942390502606,14.0570805330923));
#188841=CARTESIAN_POINT('Ctrl Pts',(19.6575305587605,17.3060450671416,14.0554647718549));
#188842=CARTESIAN_POINT('Ctrl Pts',(19.6652105839661,17.3097875357469,14.0549573550628));
#188843=CARTESIAN_POINT('Ctrl Pts',(19.6786465125811,17.3164357921098,14.0540641444558));
#188844=CARTESIAN_POINT('Ctrl Pts',(19.6844122209899,17.319321597014,14.0536790528554));
#188845=CARTESIAN_POINT('Ctrl Pts',(19.6955899894651,17.3249802041417,14.0529289624324));
#188846=CARTESIAN_POINT('Ctrl Pts',(19.7010034675988,17.3277500774828,14.0525640694502));
#188847=CARTESIAN_POINT('Ctrl Pts',(19.7139285741416,17.33443379228,14.051688941553));
#188848=CARTESIAN_POINT('Ctrl Pts',(19.7214287510232,17.3383694435991,14.0511779392764));
#188849=CARTESIAN_POINT('Ctrl Pts',(19.7484816468011,17.3527729227139,14.0493230878162));
#188850=CARTESIAN_POINT('Ctrl Pts',(19.7678926558135,17.3635025575156,14.0479699664171));
#188851=CARTESIAN_POINT('Ctrl Pts',(19.9475541077115,17.4665303970982,14.0352324439307));
#188852=CARTESIAN_POINT('Ctrl Pts',(20.09520280444,17.5791337745752,14.0230552601043));
#188853=CARTESIAN_POINT('Ctrl Pts',(20.2430067593528,17.726028210977,14.0092964186109));
#188854=CARTESIAN_POINT('Ctrl Pts',(20.2594180403768,17.7428915441871,14.0077449890224));
#188855=CARTESIAN_POINT('Ctrl Pts',(20.3186161132586,17.8057847687891,14.002068793576));
#188856=CARTESIAN_POINT('Ctrl Pts',(20.3596315623533,17.8534429292961,13.9979771299646));
#188857=CARTESIAN_POINT('Ctrl Pts',(20.4176043013201,17.9272069492926,13.9920244113195));
#188858=CARTESIAN_POINT('Ctrl Pts',(20.4362049778471,17.9519739922684,13.9900855535907));
#188859=CARTESIAN_POINT('Ctrl Pts',(20.4584130420785,17.9829366799419,13.9877430012044));
#188860=CARTESIAN_POINT('Ctrl Pts',(20.4625402568024,17.9887527084451,13.9873064269833));
#188861=CARTESIAN_POINT('Ctrl Pts',(20.4689857649277,17.9979336004706,13.9866228252507));
#188862=CARTESIAN_POINT('Ctrl Pts',(20.4713237969757,18.0012844469532,13.9863744785173));
#188863=CARTESIAN_POINT('Ctrl Pts',(20.4756896475821,18.0075803075503,13.9859100563487));
#188864=CARTESIAN_POINT('Ctrl Pts',(20.4777196827694,18.0105236558754,13.9856938343639));
#188865=CARTESIAN_POINT('Ctrl Pts',(20.4823546752132,18.0172804947185,13.9851995041577));
#188866=CARTESIAN_POINT('Ctrl Pts',(20.4849546131678,18.0210973690328,13.9849217374955));
#188867=CARTESIAN_POINT('Ctrl Pts',(20.4929700073907,18.0329476352,13.984063814347));
#188868=CARTESIAN_POINT('Ctrl Pts',(20.4983429117096,18.0410098465938,13.9834864568677));
#188869=CARTESIAN_POINT('Ctrl Pts',(20.560432242084,18.1355772482507,13.9767841755339));
#188870=CARTESIAN_POINT('Ctrl Pts',(20.6107983341497,18.2261027392679,13.9710449622374));
#188871=CARTESIAN_POINT('Ctrl Pts',(20.7059003031116,18.4310640248381,13.9586949344838));
#188872=CARTESIAN_POINT('Ctrl Pts',(20.7477123368832,18.5464300677828,13.9521325232381));
#188873=CARTESIAN_POINT('Ctrl Pts',(20.7991936628308,18.7391955852769,13.9410475846764));
#188874=CARTESIAN_POINT('Ctrl Pts',(20.8149923820532,18.8146502137216,13.9366836593196));
#188875=CARTESIAN_POINT('Ctrl Pts',(20.8295288347898,18.9096500032595,13.9310737748004));
#188876=CARTESIAN_POINT('Ctrl Pts',(20.8321591821473,18.9285448192748,13.9299525556339));
#188877=CARTESIAN_POINT('Ctrl Pts',(20.8356047515968,18.9560088431102,13.9283139653334));
#188878=CARTESIAN_POINT('Ctrl Pts',(20.836623680787,18.9645518803336,13.9278030208232));
#188879=CARTESIAN_POINT('Ctrl Pts',(20.8383161024586,18.9795168826797,13.9269057291601));
#188880=CARTESIAN_POINT('Ctrl Pts',(20.8390123460334,18.9859361995075,13.9265201044591));
#188881=CARTESIAN_POINT('Ctrl Pts',(20.8403054332555,18.9983895876167,13.9257705509034));
#188882=CARTESIAN_POINT('Ctrl Pts',(20.8409057423918,19.0044232416205,13.9254067352932));
#188883=CARTESIAN_POINT('Ctrl Pts',(20.8422761811924,19.0188251717179,13.924536727758));
#188884=CARTESIAN_POINT('Ctrl Pts',(20.8430224155299,19.0271955701967,13.9240297885932));
#188885=CARTESIAN_POINT('Ctrl Pts',(20.845521892138,19.0572542583132,13.9222045787106));
#188886=CARTESIAN_POINT('Ctrl Pts',(20.8469905259941,19.0789642636854,13.9208774168238));
#188887=CARTESIAN_POINT('Ctrl Pts',(20.857969374078,19.2893818195942,13.9079241119828));
#188888=CARTESIAN_POINT('Ctrl Pts',(20.8425067367764,19.4785067094947,13.8954650998613));
#188889=CARTESIAN_POINT('Ctrl Pts',(20.7855313284336,19.7391928083066,13.877854066994));
#188890=CARTESIAN_POINT('Ctrl Pts',(20.7646863535259,19.8143929180065,13.8727364499377));
#188891=CARTESIAN_POINT('Ctrl Pts',(20.7284012258231,19.9218505807795,13.8655102442454));
#188892=CARTESIAN_POINT('Ctrl Pts',(20.7162220169946,19.9551377662244,13.863284714015));
#188893=CARTESIAN_POINT('Ctrl Pts',(20.7004845905697,19.9950169387015,13.8606473277932));
#188894=CARTESIAN_POINT('Ctrl Pts',(20.6977207776428,20.0019139753075,13.8601922581269));
#188895=CARTESIAN_POINT('Ctrl Pts',(20.6933562019639,20.012641757818,13.8594862543055));
#188896=CARTESIAN_POINT('Ctrl Pts',(20.6917804172114,20.0164825092571,13.8592338567537));
#188897=CARTESIAN_POINT('Ctrl Pts',(20.6888298080599,20.0236143874385,13.8587658944919));
#188898=CARTESIAN_POINT('Ctrl Pts',(20.6874579778568,20.0269066430468,13.8585501589048));
#188899=CARTESIAN_POINT('Ctrl Pts',(20.684328277839,20.0343644696377,13.8580620998532));
#188900=CARTESIAN_POINT('Ctrl Pts',(20.6825653844702,20.0385278753707,13.8577900853234));
#188901=CARTESIAN_POINT('Ctrl Pts',(20.6772936931835,20.050867719686,13.8569851103267));
#188902=CARTESIAN_POINT('Ctrl Pts',(20.6737466217189,20.0590278381891,13.8564544202059));
#188903=CARTESIAN_POINT('Ctrl Pts',(20.6466785540926,20.1202400547811,13.8524840061117));
#188904=CARTESIAN_POINT('Ctrl Pts',(20.6210342341746,20.1723323084205,13.8491644717245));
#188905=CARTESIAN_POINT('Ctrl Pts',(20.5140205871321,20.3688811535557,13.8366262103916));
#188906=CARTESIAN_POINT('Ctrl Pts',(20.4179382785717,20.5046462005304,13.8278931294995));
#188907=CARTESIAN_POINT('Ctrl Pts',(20.2679994187407,20.6711129833437,13.8154666920476));
#188908=CARTESIAN_POINT('Ctrl Pts',(20.2272348983442,20.7127765934001,13.8121887185459));
#188909=CARTESIAN_POINT('Ctrl Pts',(20.1587942861343,20.7771819914443,13.8067884297344));
#188910=CARTESIAN_POINT('Ctrl Pts',(20.132168447394,20.8009967169374,13.8047108534042));
#188911=CARTESIAN_POINT('Ctrl Pts',(20.096596634695,20.831228288282,13.801958322797));
#188912=CARTESIAN_POINT('Ctrl Pts',(20.0881842859716,20.838265868815,13.8013090214884));
#188913=CARTESIAN_POINT('Ctrl Pts',(20.0743656429183,20.8496448705529,13.8002449150705));
#188914=CARTESIAN_POINT('Ctrl Pts',(20.0689919691202,20.854025717733,13.7998317172679));
#188915=CARTESIAN_POINT('Ctrl Pts',(20.0585828277422,20.8624269135181,13.7990324359482));
#188916=CARTESIAN_POINT('Ctrl Pts',(20.0535503280914,20.8664508293669,13.7986465023825));
#188917=CARTESIAN_POINT('Ctrl Pts',(20.0419374411635,20.8756497323686,13.7977570202314));
#188918=CARTESIAN_POINT('Ctrl Pts',(20.0353446031063,20.8808087621923,13.7972528427217));
#188919=CARTESIAN_POINT('Ctrl Pts',(20.0176419186016,20.8944929551246,13.7959010805419));
#188920=CARTESIAN_POINT('Ctrl Pts',(20.0064779339125,20.9029471026187,13.7950507154075));
#188921=CARTESIAN_POINT('Ctrl Pts',(19.9137396982092,20.9717379365629,13.7880029520564));
#188922=CARTESIAN_POINT('Ctrl Pts',(19.8280200849992,21.0262406666247,13.7815808505949));
#188923=CARTESIAN_POINT('Ctrl Pts',(19.588607694157,21.1553316030364,13.763925480567));
#188924=CARTESIAN_POINT('Ctrl Pts',(19.4292598333498,21.2178357167485,13.7524187033296));
#188925=CARTESIAN_POINT('Ctrl Pts',(19.2256143959061,21.2705116569355,13.7389665919713));
#188926=CARTESIAN_POINT('Ctrl Pts',(19.186806933324,21.2793905174442,13.7364598506713));
#188927=CARTESIAN_POINT('Ctrl Pts',(19.1402365375917,21.2886717436491,13.7335370918876));
#188928=CARTESIAN_POINT('Ctrl Pts',(19.1326953608763,21.2901320333729,13.7330664618871));
#188929=CARTESIAN_POINT('Ctrl Pts',(19.1210127556731,21.2923283779349,13.7323416542064));
#188930=CARTESIAN_POINT('Ctrl Pts',(19.1168768911561,21.2930931719736,13.7320858869709));
#188931=CARTESIAN_POINT('Ctrl Pts',(19.1092342581803,21.2944828866384,13.7316148208808));
#188932=CARTESIAN_POINT('Ctrl Pts',(19.1057282191044,21.2951112779483,13.7313993313013));
#188933=CARTESIAN_POINT('Ctrl Pts',(19.0978383904203,21.2965048376505,13.7309157662693));
#188934=CARTESIAN_POINT('Ctrl Pts',(19.0934537780306,21.2972650321804,13.7306479756776));
#188935=CARTESIAN_POINT('Ctrl Pts',(19.0822268559301,21.2991750872931,13.7299646219927));
#188936=CARTESIAN_POINT('Ctrl Pts',(19.0753811703667,21.3003051567227,13.7295501563365));
#188937=CARTESIAN_POINT('Ctrl Pts',(19.03532608813,21.3067152286986,13.7271373403389));
#188938=CARTESIAN_POINT('Ctrl Pts',(19.0019982179598,21.3112373608545,13.7251790415031));
#188939=CARTESIAN_POINT('Ctrl Pts',(18.9504867708261,21.3169804649612,13.7222086286926));
#188940=CARTESIAN_POINT('Ctrl Pts',(18.9323730921317,21.3187638367739,13.7211747773869));
#188941=CARTESIAN_POINT('Ctrl Pts',(18.8831230489343,21.3229721916632,13.7183874391959));
#188942=CARTESIAN_POINT('Ctrl Pts',(18.851951820444,21.3249422220241,13.7166488560521));
#188943=CARTESIAN_POINT('Ctrl Pts',(18.7822823959153,21.3277994377446,13.7127986426394));
#188944=CARTESIAN_POINT('Ctrl Pts',(18.7437805997319,21.3283274470049,13.7106950363509));
#188945=CARTESIAN_POINT('Ctrl Pts',(18.5960098968152,21.3263229053128,13.7026493474654));
#188946=CARTESIAN_POINT('Ctrl Pts',(18.4870146434121,21.3163811067843,13.6967644158466));
#188947=CARTESIAN_POINT('Ctrl Pts',(18.3250242819036,21.2888489864065,13.6876274224407));
#188948=CARTESIAN_POINT('Ctrl Pts',(18.2711535722023,21.2775164140463,13.6845241144869));
#188949=CARTESIAN_POINT('Ctrl Pts',(18.1845502059323,21.2557416764417,13.6793864490267));
#188950=CARTESIAN_POINT('Ctrl Pts',(18.1515216253027,21.2465791182312,13.6773913518622));
#188951=CARTESIAN_POINT('Ctrl Pts',(18.1083928318406,21.2334790274151,13.6747330085138));
#188952=CARTESIAN_POINT('Ctrl Pts',(18.0980786987662,21.2302597250657,13.6740932386801));
#188953=CARTESIAN_POINT('Ctrl Pts',(18.0812217051616,21.2248562685439,13.6730408217615));
#188954=CARTESIAN_POINT('Ctrl Pts',(18.0746639951562,21.2227188182128,13.6726297142945));
#188955=CARTESIAN_POINT('Ctrl Pts',(18.0619874559928,21.218518327695,13.6718316753803));
#188956=CARTESIAN_POINT('Ctrl Pts',(18.0558673834029,21.216459261169,13.6714448789351));
#188957=CARTESIAN_POINT('Ctrl Pts',(18.0417538801784,21.2116388552162,13.6705493437505));
#188958=CARTESIAN_POINT('Ctrl Pts',(18.0337674245437,21.208857566604,13.6700399481599));
#188959=CARTESIAN_POINT('Ctrl Pts',(18.0123241717683,21.201245567273,13.6686650391726));
#188960=CARTESIAN_POINT('Ctrl Pts',(17.9988994734865,21.1963263256404,13.6677965937267));
#188961=CARTESIAN_POINT('Ctrl Pts',(17.8756712562893,21.1497503246915,13.6597526880633));
#188962=CARTESIAN_POINT('Ctrl Pts',(17.7694802719312,21.0991670550833,13.6522722366108));
#188963=CARTESIAN_POINT('Ctrl Pts',(17.5265488643155,20.9575885417094,13.6339019961134));
#188964=CARTESIAN_POINT('Ctrl Pts',(17.395103842211,20.8589888241786,13.6228709531511));
#188965=CARTESIAN_POINT('Ctrl Pts',(17.2538231742291,20.7248459402256,13.6105089000861));
#188966=CARTESIAN_POINT('Ctrl Pts',(17.2317792671371,20.7029738844986,13.6085649599625));
#188967=CARTESIAN_POINT('Ctrl Pts',(17.2052685660834,20.6754863066757,13.6062171421838));
#188968=CARTESIAN_POINT('Ctrl Pts',(17.2003398505197,20.6703239834686,13.6057802132333));
#188969=CARTESIAN_POINT('Ctrl Pts',(17.1926298773146,20.6621663755025,13.6050961813666));
#188970=CARTESIAN_POINT('Ctrl Pts',(17.1898310784468,20.6591878492994,13.6048477565224));
#188971=CARTESIAN_POINT('Ctrl Pts',(17.1846001258868,20.6535885807373,13.6043832683274));
#188972=CARTESIAN_POINT('Ctrl Pts',(17.182166013534,20.650969812821,13.6041670579525));
#188973=CARTESIAN_POINT('Ctrl Pts',(17.1766043192418,20.6449557185223,13.603672858861));
#188974=CARTESIAN_POINT('Ctrl Pts',(17.1734812058476,20.6415563264513,13.6033952110307));
#188975=CARTESIAN_POINT('Ctrl Pts',(17.1638449923011,20.6309985609655,13.6025380204084));
#188976=CARTESIAN_POINT('Ctrl Pts',(17.157369735324,20.6238056051295,13.6019612697349));
#188977=CARTESIAN_POINT('Ctrl Pts',(17.088826019706,20.5466065504134,13.5958448791517));
#188978=CARTESIAN_POINT('Ctrl Pts',(17.0314059727664,20.4725943617997,13.590620166515));
#188979=CARTESIAN_POINT('Ctrl Pts',(16.9052208604029,20.285564457032,13.5782429474349));
#188980=CARTESIAN_POINT('Ctrl Pts',(16.8417781633985,20.1694460029513,13.5711935411569));
#188981=CARTESIAN_POINT('Ctrl Pts',(16.7738052630997,20.011570871112,13.561645681534));
#188982=CARTESIAN_POINT('Ctrl Pts',(16.7590846198133,19.9745349304647,13.5594100760382));
#188983=CARTESIAN_POINT('Ctrl Pts',(16.7454193601307,19.9371102111504,13.5571444941232));
#188984=CARTESIAN_POINT('',(16.61700079985,19.2129106874016,14.0892703927652));
#188985=CARTESIAN_POINT('Ctrl Pts',(16.7454193976962,19.9371103140301,13.3344632337298));
#188986=CARTESIAN_POINT('Ctrl Pts',(16.7539003396954,19.9603368629759,13.3360898566401));
#188987=CARTESIAN_POINT('Ctrl Pts',(16.7627902574051,19.9834204390165,13.3377116742357));
#188988=CARTESIAN_POINT('Ctrl Pts',(16.778326429023,20.0217439766485,13.3404079852639));
#188989=CARTESIAN_POINT('Ctrl Pts',(16.784748055774,20.0370640352716,13.3414868640114));
#188990=CARTESIAN_POINT('Ctrl Pts',(16.8125073017994,20.1011625175549,13.3460009933274));
#188991=CARTESIAN_POINT('Ctrl Pts',(16.8355026337222,20.1492069485804,13.3493852239665));
#188992=CARTESIAN_POINT('Ctrl Pts',(16.8643428899819,20.2040494547763,13.3532075480442));
#188993=CARTESIAN_POINT('Ctrl Pts',(16.8684462585545,20.2117368147759,13.3537423635551));
#188994=CARTESIAN_POINT('Ctrl Pts',(16.8747318906361,20.2233394608875,13.3545478489336));
#188995=CARTESIAN_POINT('Ctrl Pts',(16.8768792570309,20.2272734048751,13.3548206519788));
#188996=CARTESIAN_POINT('Ctrl Pts',(16.8807565588196,20.2343232375642,13.3553089461363));
#188997=CARTESIAN_POINT('Ctrl Pts',(16.8824818758396,20.2374415898167,13.3555247249163));
#188998=CARTESIAN_POINT('Ctrl Pts',(16.8862483451277,20.2442087403399,13.3559925298717));
#188999=CARTESIAN_POINT('Ctrl Pts',(16.8882924274702,20.2478558417629,13.3562443646639));
#189000=CARTESIAN_POINT('Ctrl Pts',(16.8940655501242,20.2580852168319,13.356949976287));
#189001=CARTESIAN_POINT('Ctrl Pts',(16.8978191314054,20.2646536683704,13.3574022049147));
#189002=CARTESIAN_POINT('Ctrl Pts',(16.9204919322803,20.3038400331006,13.3600958525835));
#189003=CARTESIAN_POINT('Ctrl Pts',(16.9402459327431,20.3359700403961,13.362286659183));
#189004=CARTESIAN_POINT('Ctrl Pts',(17.0081356023194,20.4400536240746,13.3693824521066));
#189005=CARTESIAN_POINT('Ctrl Pts',(17.0598276439886,20.5095877029336,13.3741230124526));
#189006=CARTESIAN_POINT('Ctrl Pts',(17.2291757262982,20.7104037404113,13.3884176297891));
#189007=CARTESIAN_POINT('Ctrl Pts',(17.3590578137782,20.8303316478873,13.3978831090112));
#189008=CARTESIAN_POINT('Ctrl Pts',(17.5209471765395,20.9461421760145,13.4094500382727));
#189009=CARTESIAN_POINT('Ctrl Pts',(17.5398248834471,20.959187991588,13.41079438881));
#189010=CARTESIAN_POINT('Ctrl Pts',(17.5668447396273,20.9772187254177,13.4127140848378));
#189011=CARTESIAN_POINT('Ctrl Pts',(17.5748146844975,20.9824596771105,13.4132797849239));
#189012=CARTESIAN_POINT('Ctrl Pts',(17.5878261075909,20.9908904448638,13.4142025612198));
#189013=CARTESIAN_POINT('Ctrl Pts',(17.5928461856283,20.9941131647152,13.41455840437));
#189014=CARTESIAN_POINT('Ctrl Pts',(17.6033862398915,21.0008167816447,13.4153051765537));
#189015=CARTESIAN_POINT('Ctrl Pts',(17.6089088165838,21.0042934544916,13.4156962571728));
#189016=CARTESIAN_POINT('Ctrl Pts',(17.6220913789668,21.0125075176604,13.4166293522862));
#189017=CARTESIAN_POINT('Ctrl Pts',(17.6297656489515,21.0172216397112,13.417172216483));
#189018=CARTESIAN_POINT('Ctrl Pts',(17.6557515302608,21.0329566432197,13.4190094166166));
#189019=CARTESIAN_POINT('Ctrl Pts',(17.6741994219889,21.0437488792938,13.4203120430282));
#189020=CARTESIAN_POINT('Ctrl Pts',(17.7757271191681,21.1010983274128,13.4274744492781));
#189021=CARTESIAN_POINT('Ctrl Pts',(17.8617021116538,21.1422821558589,13.4335232583251));
#189022=CARTESIAN_POINT('Ctrl Pts',(18.1086038735818,21.2406961341987,13.4507947346567));
#189023=CARTESIAN_POINT('Ctrl Pts',(18.2741028532549,21.2844700802679,13.4623042692789));
#189024=CARTESIAN_POINT('Ctrl Pts',(18.4794996868301,21.3129686798259,13.4755392979049));
#189025=CARTESIAN_POINT('Ctrl Pts',(18.5160720245392,21.3170746698919,13.4778537146383));
#189026=CARTESIAN_POINT('Ctrl Pts',(18.5598511791715,21.3208370076898,13.4805595869314));
#189027=CARTESIAN_POINT('Ctrl Pts',(18.5669703010171,21.3214125411374,13.4809975646307));
#189028=CARTESIAN_POINT('Ctrl Pts',(18.5785918386382,21.3222928895063,13.481709065548));
#189029=CARTESIAN_POINT('Ctrl Pts',(18.5830924898715,21.3226193516248,13.4819837584081));
#189030=CARTESIAN_POINT('Ctrl Pts',(18.5911516294114,21.323178036803,13.4824740790997));
#189031=CARTESIAN_POINT('Ctrl Pts',(18.5947096792151,21.3234156606301,13.482690005137));
#189032=CARTESIAN_POINT('Ctrl Pts',(18.6024176376,21.323910875824,13.4831565852709));
#189033=CARTESIAN_POINT('Ctrl Pts',(18.6065676965805,21.3241652315894,13.4834070563076));
#189034=CARTESIAN_POINT('Ctrl Pts',(18.6181652274313,21.3248417508475,13.4841050047214));
#189035=CARTESIAN_POINT('Ctrl Pts',(18.6256143055934,21.3252367859744,13.4845509874819));
#189036=CARTESIAN_POINT('Ctrl Pts',(18.6689407199082,21.327304859428,13.4871323597342));
#189037=CARTESIAN_POINT('Ctrl Pts',(18.70485620256,21.3281041430899,13.4892219208716));
#189038=CARTESIAN_POINT('Ctrl Pts',(18.8205018060836,21.3277339357359,13.4958377530007));
#189039=CARTESIAN_POINT('Ctrl Pts',(18.9001551293929,21.3229752779491,13.5002239971355));
#189040=CARTESIAN_POINT('Ctrl Pts',(19.1643169283449,21.2921518103999,13.5147242045843));
#189041=CARTESIAN_POINT('Ctrl Pts',(19.3456008833673,21.2462650732379,13.5246808646911));
#189042=CARTESIAN_POINT('Ctrl Pts',(19.5390202448045,21.1690902638659,13.5367933152873));
#189043=CARTESIAN_POINT('Ctrl Pts',(19.559368046502,21.1606006283222,13.5380857808929));
#189044=CARTESIAN_POINT('Ctrl Pts',(19.5873252689255,21.1484200319878,13.5398884609172));
#189045=CARTESIAN_POINT('Ctrl Pts',(19.595051174637,21.1449987762264,13.540389497355));
#189046=CARTESIAN_POINT('Ctrl Pts',(19.6082967122084,21.1390381664547,13.5412535248257));
#189047=CARTESIAN_POINT('Ctrl Pts',(19.6138263130478,21.1365211164693,13.5416157477331));
#189048=CARTESIAN_POINT('Ctrl Pts',(19.6252042152479,21.131282701779,13.5423642418551));
#189049=CARTESIAN_POINT('Ctrl Pts',(19.6310510612237,21.1285583433513,13.5427506134777));
#189050=CARTESIAN_POINT('Ctrl Pts',(19.6446293086184,21.1221558191953,13.5436519873502));
#189051=CARTESIAN_POINT('Ctrl Pts',(19.6523509886666,21.1184574074432,13.544167687902));
#189052=CARTESIAN_POINT('Ctrl Pts',(19.6769987187309,21.1064676604585,13.5458239102111));
#189053=CARTESIAN_POINT('Ctrl Pts',(19.6938361957013,21.0979972646336,13.5469706571928));
#189054=CARTESIAN_POINT('Ctrl Pts',(19.7774009929147,21.0545506816856,13.5527406683659));
#189055=CARTESIAN_POINT('Ctrl Pts',(19.8423340491591,21.0162584893286,13.5574803416403));
#189056=CARTESIAN_POINT('Ctrl Pts',(19.9960270681439,20.9142012426487,13.5693363514648));
#189057=CARTESIAN_POINT('Ctrl Pts',(20.0821575241264,20.8468712088598,13.5765525170721));
#189058=CARTESIAN_POINT('Ctrl Pts',(20.173810868615,20.7630503084306,13.5847573911428));
#189059=CARTESIAN_POINT('Ctrl Pts',(20.1848080757816,20.7527754143141,13.5857510360998));
#189060=CARTESIAN_POINT('Ctrl Pts',(20.270733525578,20.6707602058841,13.5935832201779));
#189061=CARTESIAN_POINT('Ctrl Pts',(20.3404157484905,20.5937086994145,13.600357954239));
#189062=CARTESIAN_POINT('Ctrl Pts',(20.410126095196,20.5042069294113,13.6073671091355));
#189063=CARTESIAN_POINT('Ctrl Pts',(20.4160265005179,20.4965231265975,13.6079623404633));
#189064=CARTESIAN_POINT('Ctrl Pts',(20.4246614949996,20.485116963178,13.6088360253738));
#189065=CARTESIAN_POINT('Ctrl Pts',(20.4274368862186,20.4814258498077,13.6091172401474));
#189066=CARTESIAN_POINT('Ctrl Pts',(20.432339644543,20.4748608452034,13.6096146808992));
#189067=CARTESIAN_POINT('Ctrl Pts',(20.4344718292198,20.4719906197009,13.6098312412901));
#189068=CARTESIAN_POINT('Ctrl Pts',(20.4390250091338,20.4658288381279,13.610294171884));
#189069=CARTESIAN_POINT('Ctrl Pts',(20.4414437432643,20.4625356802768,13.6105403855738));
#189070=CARTESIAN_POINT('Ctrl Pts',(20.4480580359774,20.4534753163946,13.6112145628692));
#189071=CARTESIAN_POINT('Ctrl Pts',(20.4522340542121,20.4476938185299,13.6116411926444));
#189072=CARTESIAN_POINT('Ctrl Pts',(20.4743895766033,20.4166916907396,13.6139105560617));
#189073=CARTESIAN_POINT('Ctrl Pts',(20.4918441937073,20.3910984493655,13.6157194443718));
#189074=CARTESIAN_POINT('Ctrl Pts',(20.5978762550671,20.2280505292606,13.6269060181742));
#189075=CARTESIAN_POINT('Ctrl Pts',(20.6708484891867,20.0810900805629,13.6355484850038));
#189076=CARTESIAN_POINT('Ctrl Pts',(20.7660124005701,19.8163750923714,13.6509436360795));
#189077=CARTESIAN_POINT('Ctrl Pts',(20.7965275074375,19.70245531893,13.657513959608));
#189078=CARTESIAN_POINT('Ctrl Pts',(20.8199515684283,19.5725239763471,13.6652483632143));
#189079=CARTESIAN_POINT('Ctrl Pts',(20.8223461988445,19.5584243372723,13.6660905416018));
#189080=CARTESIAN_POINT('Ctrl Pts',(20.8259293856213,19.5359492025367,13.667437993831));
#189081=CARTESIAN_POINT('Ctrl Pts',(20.827210943084,19.5275888236214,13.6679403204371));
#189082=CARTESIAN_POINT('Ctrl Pts',(20.8293825031154,19.5128325088085,13.6688289611689));
#189083=CARTESIAN_POINT('Ctrl Pts',(20.8302934111599,19.5064397242033,13.6692146081685));
#189084=CARTESIAN_POINT('Ctrl Pts',(20.8321167014959,19.4932106891604,13.6700140735056));
#189085=CARTESIAN_POINT('Ctrl Pts',(20.8330249520295,19.4863739551574,13.6704280176326));
#189086=CARTESIAN_POINT('Ctrl Pts',(20.8352700575238,19.4688174645755,13.6714930735985));
#189087=CARTESIAN_POINT('Ctrl Pts',(20.8365582846678,19.4580917895982,13.6721457124233));
#189088=CARTESIAN_POINT('Ctrl Pts',(20.8415887317162,19.4133168067981,13.6748787015432));
#189089=CARTESIAN_POINT('Ctrl Pts',(20.8445861876299,19.3791906109529,13.6769823177131));
#189090=CARTESIAN_POINT('Ctrl Pts',(20.8502353962861,19.2901259962246,13.6825292568718));
#189091=CARTESIAN_POINT('Ctrl Pts',(20.8515764341003,19.2351330748311,13.6860108355322));
#189092=CARTESIAN_POINT('Ctrl Pts',(20.8491826577452,19.070863536987,13.6965697907205));
#189093=CARTESIAN_POINT('Ctrl Pts',(20.8391284433405,18.9618681622872,13.7037955929223));
#189094=CARTESIAN_POINT('Ctrl Pts',(20.8142500506204,18.8163915763883,13.7135450818054));
#189095=CARTESIAN_POINT('Ctrl Pts',(20.8067700065764,18.7788186944954,13.7160714495894));
#189096=CARTESIAN_POINT('Ctrl Pts',(20.7910541040252,18.7097243646693,13.7207138084502));
#189097=CARTESIAN_POINT('Ctrl Pts',(20.7831020828263,18.6781495066885,13.7228338721764));
#189098=CARTESIAN_POINT('Ctrl Pts',(20.7732481429362,18.6425147320147,13.7252166317415));
#189099=CARTESIAN_POINT('Ctrl Pts',(20.7720582439457,18.6382635133447,13.7255007316984));
#189100=CARTESIAN_POINT('Ctrl Pts',(20.7585621250297,18.5906198369151,13.7286826153294));
#189101=CARTESIAN_POINT('Ctrl Pts',(20.7448844327948,18.5476239352467,13.7315352640544));
#189102=CARTESIAN_POINT('Ctrl Pts',(20.7273100167727,18.4979348895437,13.7347840761101));
#189103=CARTESIAN_POINT('Ctrl Pts',(20.7247391459878,18.4907886898145,13.7352501353234));
#189104=CARTESIAN_POINT('Ctrl Pts',(20.7205496049323,18.4793369480718,13.7359949171625));
#189105=CARTESIAN_POINT('Ctrl Pts',(20.7189552890664,18.475022652698,13.7362750290916));
#189106=CARTESIAN_POINT('Ctrl Pts',(20.7160942986645,18.4673575976407,13.7367718040655));
#189107=CARTESIAN_POINT('Ctrl Pts',(20.7148331664703,18.4640048201577,13.7369887931799));
#189108=CARTESIAN_POINT('Ctrl Pts',(20.7121279558111,18.4568679196462,13.7374500241156));
#189109=CARTESIAN_POINT('Ctrl Pts',(20.7106815297367,18.4530847443078,13.7376941229961));
#189110=CARTESIAN_POINT('Ctrl Pts',(20.7067163363,18.4428022119732,13.7383565631728));
#189111=CARTESIAN_POINT('Ctrl Pts',(20.7041762872266,18.4363110395993,13.7387736470407));
#189112=CARTESIAN_POINT('Ctrl Pts',(20.6909685359419,18.4030433674154,13.7409061351704));
#189113=CARTESIAN_POINT('Ctrl Pts',(20.6797862932525,18.3764727937712,13.7425923472838));
#189114=CARTESIAN_POINT('Ctrl Pts',(20.6451739145466,18.2987105960817,13.7475001041646));
#189115=CARTESIAN_POINT('Ctrl Pts',(20.620239819818,18.2482134616489,13.7506519864536));
#189116=CARTESIAN_POINT('Ctrl Pts',(20.5266220544944,18.0762515956244,13.7614589364468));
#189117=CARTESIAN_POINT('Ctrl Pts',(20.447977809262,17.9606282432826,13.7688802422141));
#189118=CARTESIAN_POINT('Ctrl Pts',(20.3015038893652,17.7853316556721,13.7815347066276));
#189119=CARTESIAN_POINT('Ctrl Pts',(20.240240275257,17.7207529912661,13.7865673865744));
#189120=CARTESIAN_POINT('Ctrl Pts',(20.1650751246328,17.65090373097,13.792583393331));
#189121=CARTESIAN_POINT('Ctrl Pts',(20.1549576889409,17.6416830740437,13.7933899720032));
#189122=CARTESIAN_POINT('Ctrl Pts',(20.1385787850756,17.6270441986982,13.794691034061));
#189123=CARTESIAN_POINT('Ctrl Pts',(20.132373610447,17.621563374464,13.7951828827188));
#189124=CARTESIAN_POINT('Ctrl Pts',(20.1212928442631,17.6118912167137,13.7960593990968));
#189125=CARTESIAN_POINT('Ctrl Pts',(20.1164299827331,17.6076854089232,13.7964434581492));
#189126=CARTESIAN_POINT('Ctrl Pts',(20.1062519413445,17.5989633202575,13.7972460828253));
#189127=CARTESIAN_POINT('Ctrl Pts',(20.1009334569397,17.5944510307923,13.7976648062452));
#189128=CARTESIAN_POINT('Ctrl Pts',(20.0870500383865,17.5827896140155,13.7987561329551));
#189129=CARTESIAN_POINT('Ctrl Pts',(20.0784507993602,17.5756818327794,13.7994304111367));
#189130=CARTESIAN_POINT('Ctrl Pts',(20.0407323987774,17.5450039299075,13.8023810371507));
#189131=CARTESIAN_POINT('Ctrl Pts',(20.0110481228621,17.5221423155561,13.8046855355722));
#189132=CARTESIAN_POINT('Ctrl Pts',(19.9304354458203,17.4633985409742,13.8109017915333));
#189133=CARTESIAN_POINT('Ctrl Pts',(19.878506296171,17.4289582442609,13.8148643232619));
#189134=CARTESIAN_POINT('Ctrl Pts',(19.7241741389192,17.3361331764053,13.8265040618338));
#189135=CARTESIAN_POINT('Ctrl Pts',(19.6183212974585,17.2839444868769,13.8343344223526));
#189136=CARTESIAN_POINT('Ctrl Pts',(19.4168669268243,17.2047307756767,13.848593214044));
#189137=CARTESIAN_POINT('Ctrl Pts',(19.3226236843964,17.1750849185475,13.8550208566877));
#189138=CARTESIAN_POINT('Ctrl Pts',(19.2172178562941,17.1498635442951,13.86171714985));
#189139=CARTESIAN_POINT('Ctrl Pts',(19.2077737958847,17.1476722547751,13.8623128189293));
#189140=CARTESIAN_POINT('Ctrl Pts',(19.1938078561854,17.1445327066358,13.8631870213125));
#189141=CARTESIAN_POINT('Ctrl Pts',(19.1892975468645,17.1435342847083,13.8634683204302));
#189142=CARTESIAN_POINT('Ctrl Pts',(19.1812903074939,17.1417892407711,13.863965854421));
#189143=CARTESIAN_POINT('Ctrl Pts',(19.1777947212744,17.1410367077324,13.8641824241736));
#189144=CARTESIAN_POINT('Ctrl Pts',(19.170301431827,17.13944339968,13.8646453128906));
#189145=CARTESIAN_POINT('Ctrl Pts',(19.1663032078698,17.1386053404677,13.8648914756652));
#189146=CARTESIAN_POINT('Ctrl Pts',(19.1553220451363,17.136336764372,13.8655653698979));
#189147=CARTESIAN_POINT('Ctrl Pts',(19.1483341941905,17.1349299178979,13.8659917693912));
#189148=CARTESIAN_POINT('Ctrl Pts',(19.1109978553072,17.1276091073585,13.8682577097136));
#189149=CARTESIAN_POINT('Ctrl Pts',(19.0805279392286,17.1223249154687,13.8700635260463));
#189150=CARTESIAN_POINT('Ctrl Pts',(18.9879673209267,17.1083542481792,13.8754479324895));
#189151=CARTESIAN_POINT('Ctrl Pts',(18.9255935183328,17.1017556732976,13.8789398135878));
#189152=CARTESIAN_POINT('Ctrl Pts',(18.7042738212957,17.0882428403205,13.8911259296222));
#189153=CARTESIAN_POINT('Ctrl Pts',(18.5449519477682,17.0964686433019,13.8995686527687));
#189154=CARTESIAN_POINT('Ctrl Pts',(18.3259805325961,17.1327392627767,13.9120550465058));
#189155=CARTESIAN_POINT('Ctrl Pts',(18.2644032900513,17.1457819947166,13.9156608522928));
#189156=CARTESIAN_POINT('Ctrl Pts',(18.1914221174167,17.1646730608851,13.9200881445245));
#189157=CARTESIAN_POINT('Ctrl Pts',(18.1793703310514,17.1679066049849,13.9208242970885));
#189158=CARTESIAN_POINT('Ctrl Pts',(18.1596372602922,17.1733885336909,13.922038240547));
#189159=CARTESIAN_POINT('Ctrl Pts',(18.1519387870102,17.1755742985697,13.9225139968257));
#189160=CARTESIAN_POINT('Ctrl Pts',(18.138126582831,17.1795806535486,13.923371535924));
#189161=CARTESIAN_POINT('Ctrl Pts',(18.1320083092197,17.1813853337935,13.9237527955555));
#189162=CARTESIAN_POINT('Ctrl Pts',(18.1190018681884,17.185285771294,13.9245663209507));
#189163=CARTESIAN_POINT('Ctrl Pts',(18.112116062618,17.1873890677935,13.9249988296368));
#189164=CARTESIAN_POINT('Ctrl Pts',(18.0936177046689,17.193142796919,13.9261657008433));
#189165=CARTESIAN_POINT('Ctrl Pts',(18.0820258177424,17.1968582889558,13.9269021919542));
#189166=CARTESIAN_POINT('Ctrl Pts',(18.0251375826535,17.2156349563827,13.9305431139578));
#189167=CARTESIAN_POINT('Ctrl Pts',(17.9803305235137,17.2321242264999,13.93349440139));
#189168=CARTESIAN_POINT('Ctrl Pts',(17.7806194787107,17.3133859656406,13.9470404614779));
#189169=CARTESIAN_POINT('Ctrl Pts',(17.6332142049446,17.394925243404,13.9581913930841));
#189170=CARTESIAN_POINT('Ctrl Pts',(17.416849188789,17.5507107443981,13.9757536987232));
#189171=CARTESIAN_POINT('Ctrl Pts',(17.3408135752584,17.613976866279,13.9821893792898));
#189172=CARTESIAN_POINT('Ctrl Pts',(17.2624671936725,17.6890360758549,13.9888929470817));
#189173=CARTESIAN_POINT('Ctrl Pts',(17.2555127444208,17.6957909616849,13.989488618792));
#189174=CARTESIAN_POINT('Ctrl Pts',(17.2453133466887,17.7058347640599,13.9903628242852));
#189175=CARTESIAN_POINT('Ctrl Pts',(17.242032481042,17.7090867992664,13.9906441239097));
#189176=CARTESIAN_POINT('Ctrl Pts',(17.2362310019053,17.7148750675029,13.9911416584608));
#189177=CARTESIAN_POINT('Ctrl Pts',(17.2337061455294,17.7174069710225,13.9913582282698));
#189178=CARTESIAN_POINT('Ctrl Pts',(17.2283104530683,17.7228452110206,13.9918211167355));
#189179=CARTESIAN_POINT('Ctrl Pts',(17.2254416186569,17.7257534553381,13.9920672792045));
#189180=CARTESIAN_POINT('Ctrl Pts',(17.219571729999,17.7317385330182,13.9925710976025));
#189181=CARTESIAN_POINT('Ctrl Pts',(17.2165715894308,17.7348162403675,13.9928286828565));
#189182=CARTESIAN_POINT('Ctrl Pts',(17.2028282053979,17.7490011216773,13.9940091496748));
#189183=CARTESIAN_POINT('Ctrl Pts',(17.1921970803482,17.7602169104497,13.994923679733));
#189184=CARTESIAN_POINT('Ctrl Pts',(17.1270839219106,17.8304352159113,14.0005412505477));
#189185=CARTESIAN_POINT('Ctrl Pts',(17.0758674163161,17.8923880458916,14.0050328575433));
#189186=CARTESIAN_POINT('Ctrl Pts',(16.9870844287355,18.0131623280466,14.0132735216999));
#189187=CARTESIAN_POINT('Ctrl Pts',(16.9486652663682,18.0712152024473,14.017036525318));
#189188=CARTESIAN_POINT('Ctrl Pts',(16.8366942178351,18.2600025000754,14.0289657726126));
#189189=CARTESIAN_POINT('Ctrl Pts',(16.7741390012416,18.3966891816244,14.037197792598));
#189190=CARTESIAN_POINT('Ctrl Pts',(16.7220478750628,18.5522600454468,14.0468105579356));
#189191=CARTESIAN_POINT('Ctrl Pts',(16.7176849722239,18.5657377471158,14.0476448800404));
#189192=CARTESIAN_POINT('Ctrl Pts',(16.7109454564795,18.5872931858504,14.0489821065602));
#189193=CARTESIAN_POINT('Ctrl Pts',(16.7084811540861,18.5953432142828,14.04948213411));
#189194=CARTESIAN_POINT('Ctrl Pts',(16.7042134851124,18.6095872305298,14.0503681000156));
#189195=CARTESIAN_POINT('Ctrl Pts',(16.7023902813161,18.6157751980733,14.0507533841226));
#189196=CARTESIAN_POINT('Ctrl Pts',(16.6986719539506,18.6286113546009,14.0515534710001));
#189197=CARTESIAN_POINT('Ctrl Pts',(16.6967810570501,18.6352606787376,14.0519684063414));
#189198=CARTESIAN_POINT('Ctrl Pts',(16.6919990650989,18.6523950626001,14.0530389220398));
#189199=CARTESIAN_POINT('Ctrl Pts',(16.6891561701449,18.6628932596528,14.0536960597197));
#189200=CARTESIAN_POINT('Ctrl Pts',(16.6831808523557,18.6856525316541,14.055123505956));
#189201=CARTESIAN_POINT('Ctrl Pts',(16.6800772339591,18.6979206698156,14.0558947188747));
#189202=CARTESIAN_POINT('Ctrl Pts',(16.6713661332148,18.7337005525461,14.0581493256177));
#189203=CARTESIAN_POINT('Ctrl Pts',(16.6660512434075,18.7572808182923,14.0596419400709));
#189204=CARTESIAN_POINT('Ctrl Pts',(16.631655751107,18.9230670248615,14.0701853398582));
#189205=CARTESIAN_POINT('Ctrl Pts',(16.6168699503979,19.0678169686808,14.0796830582003));
#189206=CARTESIAN_POINT('Ctrl Pts',(16.6170008616904,19.2129100775731,14.0892704606451));
#189207=CARTESIAN_POINT('Ctrl Pts',(16.6170008622342,19.2129106802283,14.0892705004671));
#189208=CARTESIAN_POINT('Ctrl Pts',(16.6171115220818,19.3355197900838,14.0973722145855));
#189209=CARTESIAN_POINT('Ctrl Pts',(16.627873578249,19.4579019708157,14.1054939081815));
#189210=CARTESIAN_POINT('Ctrl Pts',(16.6513555158085,19.5910511198309,14.1139585279377));
#189211=CARTESIAN_POINT('Ctrl Pts',(16.6536481259094,19.6034066737466,14.1147402688335));
#189212=CARTESIAN_POINT('Ctrl Pts',(16.6573287572654,19.6223030987319,14.1159293748916));
#189213=CARTESIAN_POINT('Ctrl Pts',(16.6586379331589,19.6288588082238,14.1163407108087));
#189214=CARTESIAN_POINT('Ctrl Pts',(16.6608486766564,19.6396623911444,14.1170164748051));
#189215=CARTESIAN_POINT('Ctrl Pts',(16.661732288431,19.6439138337036,14.1172818639948));
#189216=CARTESIAN_POINT('Ctrl Pts',(16.6634789761593,19.6521900187716,14.1177974009758));
#189217=CARTESIAN_POINT('Ctrl Pts',(16.6643407213195,19.6562150195898,14.1180476216642));
#189218=CARTESIAN_POINT('Ctrl Pts',(16.665971986405,19.6637271660026,14.1185136530072));
#189219=CARTESIAN_POINT('Ctrl Pts',(16.6667385816777,19.6672148401818,14.1187296215364));
#189220=CARTESIAN_POINT('Ctrl Pts',(16.6685067296659,19.6751631716213,14.119220920855));
#189221=CARTESIAN_POINT('Ctrl Pts',(16.6695139067983,19.6796225256659,14.1194959257347));
#189222=CARTESIAN_POINT('Ctrl Pts',(16.6726472977642,19.6932896848048,14.1203369169667));
#189223=CARTESIAN_POINT('Ctrl Pts',(16.6748207595118,19.7024866896663,14.1209002613306));
#189224=CARTESIAN_POINT('Ctrl Pts',(16.6956478218852,19.7880524097973,14.1261199400262));
#189225=CARTESIAN_POINT('Ctrl Pts',(16.7184739237694,19.8633153988605,14.1305523033505));
#189226=CARTESIAN_POINT('Ctrl Pts',(16.7454193878426,19.9371102870445,14.1348940376456));
#189227=CARTESIAN_POINT('Origin',(18.734,19.211,0.));
#189228=CARTESIAN_POINT('',(16.7454193623258,19.9371102171621,15.155594536163));
#189229=CARTESIAN_POINT('',(16.7454193857226,19.9371102812384,14.9318514580964));
#189230=CARTESIAN_POINT('',(16.7454193623258,19.9371102171621,0.));
#189231=CARTESIAN_POINT('',(16.6156459487826,19.212740575031,15.1109429532718));
#189232=CARTESIAN_POINT('Ctrl Pts',(16.6170007251258,19.2127521935258,15.1109437209775));
#189233=CARTESIAN_POINT('Ctrl Pts',(16.6170993834537,19.3319511321298,15.1181312937192));
#189234=CARTESIAN_POINT('Ctrl Pts',(16.6272689227094,19.4507453566806,15.1253188664609));
#189235=CARTESIAN_POINT('Ctrl Pts',(16.6472858251195,19.5678094062,15.1325064392026));
#189236=CARTESIAN_POINT('Ctrl Pts',(16.659503668485,19.6392625307373,15.1368935634507));
#189237=CARTESIAN_POINT('Ctrl Pts',(16.675419638095,19.7102268266389,15.1412806876989));
#189238=CARTESIAN_POINT('Ctrl Pts',(16.6949811994265,19.7802901992024,15.145667811947));
#189239=CARTESIAN_POINT('Ctrl Pts',(16.7097351486035,19.833134214077,15.148976720019));
#189240=CARTESIAN_POINT('Ctrl Pts',(16.7265618764294,19.8854656727906,15.152285628091));
#189241=CARTESIAN_POINT('Ctrl Pts',(16.7454193623258,19.9371102171621,15.155594536163));
#189242=CARTESIAN_POINT('Ctrl Pts',(16.7430900140495,19.9379407811485,14.3554399645868));
#189243=CARTESIAN_POINT('Ctrl Pts',(16.7690653364714,20.0108542721151,14.3601105094292));
#189244=CARTESIAN_POINT('Ctrl Pts',(17.0725680194683,20.7297352289216,14.407172989832));
#189245=CARTESIAN_POINT('Ctrl Pts',(18.453125516026,21.6984565773648,14.4966274057954));
#189246=CARTESIAN_POINT('Ctrl Pts',(20.6735253020556,20.7935840586525,14.6238032124768));
#189247=CARTESIAN_POINT('Ctrl Pts',(21.114531003966,18.4367888923735,14.7509790191583));
#189248=CARTESIAN_POINT('Ctrl Pts',(19.3715472621554,16.7902843643798,14.8781548258396));
#189249=CARTESIAN_POINT('Ctrl Pts',(17.1752233264884,17.3321744887536,14.9981428038775));
#189250=CARTESIAN_POINT('Ctrl Pts',(16.6208559023486,18.6285361102004,15.0757388463549));
#189251=CARTESIAN_POINT('Ctrl Pts',(16.6156459487826,19.212740575031,15.1109429532718));
#189252=CARTESIAN_POINT('Ctrl Pts',(16.7454193878426,19.9371102870445,14.1348940376456));
#189253=CARTESIAN_POINT('Ctrl Pts',(16.7604972143715,19.9784035644483,14.1373235343638));
#189254=CARTESIAN_POINT('Ctrl Pts',(16.7768648728234,20.0192371694941,14.1397244633557));
#189255=CARTESIAN_POINT('Ctrl Pts',(16.8230771657304,20.124862769637,14.1459966983079));
#189256=CARTESIAN_POINT('Ctrl Pts',(16.8549327852444,20.1886898818392,14.1498507198238));
#189257=CARTESIAN_POINT('Ctrl Pts',(16.9337290706316,20.3284343335731,14.1586405514275));
#189258=CARTESIAN_POINT('Ctrl Pts',(16.9823674089659,20.4032314873514,14.1635988479836));
#189259=CARTESIAN_POINT('Ctrl Pts',(17.0559411465615,20.5021126425508,14.1706897807959));
#189260=CARTESIAN_POINT('Ctrl Pts',(17.0769686928333,20.5289910565066,14.1726760533279));
#189261=CARTESIAN_POINT('Ctrl Pts',(17.1055473282265,20.5637562066665,14.1753299197156));
#189262=CARTESIAN_POINT('Ctrl Pts',(17.1125235035304,20.5721103642186,14.1759743089135));
#189263=CARTESIAN_POINT('Ctrl Pts',(17.1240365248426,20.5856833893665,14.1770323897217));
#189264=CARTESIAN_POINT('Ctrl Pts',(17.1285351250224,20.5909345440311,14.1774445090444));
#189265=CARTESIAN_POINT('Ctrl Pts',(17.1372798274166,20.6010414733071,14.1782431375107));
#189266=CARTESIAN_POINT('Ctrl Pts',(17.1415225602354,20.6059000714965,14.1786295043654));
#189267=CARTESIAN_POINT('Ctrl Pts',(17.1513511886196,20.6170521146089,14.1795220529518));
#189268=CARTESIAN_POINT('Ctrl Pts',(17.1569525081977,20.6233317650491,14.1800288777588));
#189269=CARTESIAN_POINT('Ctrl Pts',(17.1720744996244,20.640082931504,14.1813923661629));
#189270=CARTESIAN_POINT('Ctrl Pts',(17.1816628618323,20.6504925105874,14.1822518865271));
#189271=CARTESIAN_POINT('Ctrl Pts',(17.2658131808938,20.7400315153285,14.1897533493696));
#189272=CARTESIAN_POINT('Ctrl Pts',(17.3462525661143,20.8133921541756,14.1966548188598));
#189273=CARTESIAN_POINT('Ctrl Pts',(17.5089838418746,20.9403256574057,14.2100930077399));
#189274=CARTESIAN_POINT('Ctrl Pts',(17.590073873907,20.9950020741772,14.2165775281884));
#189275=CARTESIAN_POINT('Ctrl Pts',(17.7368998283904,21.0798634730265,14.2277552108006));
#189276=CARTESIAN_POINT('Ctrl Pts',(17.8009525811308,21.11265280255,14.2324604630758));
#189277=CARTESIAN_POINT('Ctrl Pts',(17.89726551958,21.1559159188901,14.239177042908));
#189278=CARTESIAN_POINT('Ctrl Pts',(17.9283039878583,21.1689777206307,14.2412890188647));
#189279=CARTESIAN_POINT('Ctrl Pts',(17.966423615382,21.1839593447083,14.2438082347667));
#189280=CARTESIAN_POINT('Ctrl Pts',(17.9732182939624,21.1865893503975,14.2442544297581));
#189281=CARTESIAN_POINT('Ctrl Pts',(17.9839067656961,21.19066319947,14.244951711349));
#189282=CARTESIAN_POINT('Ctrl Pts',(17.987791385608,21.1921307246054,14.2452041790916));
#189283=CARTESIAN_POINT('Ctrl Pts',(17.9950204383038,21.1948374247086,14.2456722045895));
#189284=CARTESIAN_POINT('Ctrl Pts',(17.9983636520336,21.1960795661886,14.2458879336391));
#189285=CARTESIAN_POINT('Ctrl Pts',(18.0059506888618,21.1988766630714,14.2463758926936));
#189286=CARTESIAN_POINT('Ctrl Pts',(18.0101963513963,21.200426476694,14.246647814292));
#189287=CARTESIAN_POINT('Ctrl Pts',(18.0228078148333,21.2049843805099,14.2474522596417));
#189288=CARTESIAN_POINT('Ctrl Pts',(18.0311877564427,21.2079534272303,14.2479825174769));
#189289=CARTESIAN_POINT('Ctrl Pts',(18.0942142684581,21.2298380896441,14.2519404117078));
#189290=CARTESIAN_POINT('Ctrl Pts',(18.1496018238592,21.2465620977439,14.2552487130249));
#189291=CARTESIAN_POINT('Ctrl Pts',(18.3636351368334,21.30172952605,14.2676340742042));
#189292=CARTESIAN_POINT('Ctrl Pts',(18.525845624908,21.3240542411295,14.2762395421047));
#189293=CARTESIAN_POINT('Ctrl Pts',(18.7490765715584,21.3287984505572,14.288607272365));
#189294=CARTESIAN_POINT('Ctrl Pts',(18.8091576894109,21.3275179188448,14.291982319262));
#189295=CARTESIAN_POINT('Ctrl Pts',(18.8932438317346,21.3221408546444,14.2968207419258));
#189296=CARTESIAN_POINT('Ctrl Pts',(18.9173586424913,21.3201832179767,14.2982215052839));
#189297=CARTESIAN_POINT('Ctrl Pts',(18.959416452345,21.3160422629032,14.3006905156906));
#189298=CARTESIAN_POINT('Ctrl Pts',(18.9773751301975,21.3140416119535,14.3017530881889));
#189299=CARTESIAN_POINT('Ctrl Pts',(19.0037769080168,21.3107576748974,14.3033283026308));
#189300=CARTESIAN_POINT('Ctrl Pts',(19.0122416728109,21.3096527682407,14.3038353223592));
#189301=CARTESIAN_POINT('Ctrl Pts',(19.0270866000763,21.3076236674702,14.3047280746367));
#189302=CARTESIAN_POINT('Ctrl Pts',(19.0334696937367,21.3067214650938,14.305113107244));
#189303=CARTESIAN_POINT('Ctrl Pts',(19.0458676887262,21.3049113036467,14.3058632622771));
#189304=CARTESIAN_POINT('Ctrl Pts',(19.0518829990925,21.304006545737,14.3062282797058));
#189305=CARTESIAN_POINT('Ctrl Pts',(19.0662722041711,21.3017788152655,14.3071039973782));
#189306=CARTESIAN_POINT('Ctrl Pts',(19.0746421661294,21.3004314497996,14.3076154673089));
#189307=CARTESIAN_POINT('Ctrl Pts',(19.104927350662,21.2953694428493,14.3094737956557));
#189308=CARTESIAN_POINT('Ctrl Pts',(19.1267912246479,21.2913600814466,14.3108299716777));
#189309=CARTESIAN_POINT('Ctrl Pts',(19.3294001659426,21.2508982346035,14.3235375821658));
#189310=CARTESIAN_POINT('Ctrl Pts',(19.5046886100218,21.1913277891537,14.3356764651532));
#189311=CARTESIAN_POINT('Ctrl Pts',(19.7426167457967,21.074044525038,14.3531918001493));
#189312=CARTESIAN_POINT('Ctrl Pts',(19.8131208857484,21.0341134080646,14.358512757353));
#189313=CARTESIAN_POINT('Ctrl Pts',(19.9116319769776,20.9705981750519,14.3659859985934));
#189314=CARTESIAN_POINT('Ctrl Pts',(19.9415882031334,20.9501762149821,14.3682635995435));
#189315=CARTESIAN_POINT('Ctrl Pts',(19.9770768281583,20.924623336678,14.3709540966073));
#189316=CARTESIAN_POINT('Ctrl Pts',(19.9831233942394,20.9202207846012,14.3714122236791));
#189317=CARTESIAN_POINT('Ctrl Pts',(19.9924983189658,20.9133185085879,14.3721219254567));
#189318=CARTESIAN_POINT('Ctrl Pts',(19.9958427830626,20.9108409087447,14.3723749879964));
#189319=CARTESIAN_POINT('Ctrl Pts',(20.0020387222181,20.9062225553543,14.3728435521985));
#189320=CARTESIAN_POINT('Ctrl Pts',(20.0048920692146,20.9040844816232,14.3730592286806));
#189321=CARTESIAN_POINT('Ctrl Pts',(20.0113396124558,20.8992277165988,14.3735463528807));
#189322=CARTESIAN_POINT('Ctrl Pts',(20.0149305281977,20.8965047586509,14.3738174966156));
#189323=CARTESIAN_POINT('Ctrl Pts',(20.0257640163184,20.8882352084294,14.3746351309585));
#189324=CARTESIAN_POINT('Ctrl Pts',(20.0329795673664,20.8826531663523,14.3751791886612));
#189325=CARTESIAN_POINT('Ctrl Pts',(20.0884676587009,20.8391506455105,14.3793609384994));
#189326=CARTESIAN_POINT('Ctrl Pts',(20.1351111125707,20.7991896299486,14.3828640790201));
#189327=CARTESIAN_POINT('Ctrl Pts',(20.2872053214426,20.6569610465483,14.3945009486614));
#189328=CARTESIAN_POINT('Ctrl Pts',(20.3837334068908,20.545778771863,14.402287180207));
#189329=CARTESIAN_POINT('Ctrl Pts',(20.5211937784511,20.3495214445373,14.4154842682804));
#189330=CARTESIAN_POINT('Ctrl Pts',(20.5693504592298,20.2701404504339,14.4206926457152));
#189331=CARTESIAN_POINT('Ctrl Pts',(20.6218690633925,20.1691667601624,14.4273222593103));
#189332=CARTESIAN_POINT('Ctrl Pts',(20.631313697697,20.1503262617893,14.4285591337442));
#189333=CARTESIAN_POINT('Ctrl Pts',(20.6443687918004,20.1232830094818,14.43033565602));
#189334=CARTESIAN_POINT('Ctrl Pts',(20.648211075904,20.1151931006188,14.4308672380318));
#189335=CARTESIAN_POINT('Ctrl Pts',(20.6547602396822,20.1011750215481,14.431788700917));
#189336=CARTESIAN_POINT('Ctrl Pts',(20.6574913121641,20.0952582416335,14.4321777391962));
#189337=CARTESIAN_POINT('Ctrl Pts',(20.6626744793243,20.0838914409243,14.4329253664322));
#189338=CARTESIAN_POINT('Ctrl Pts',(20.665130903714,20.078443454306,14.4332838016399));
#189339=CARTESIAN_POINT('Ctrl Pts',(20.6714720421519,20.064219313838,14.4342199512762));
#189340=CARTESIAN_POINT('Ctrl Pts',(20.6753201696147,20.0554270873963,14.4347989125022));
#189341=CARTESIAN_POINT('Ctrl Pts',(20.6883060531377,20.025198898276,14.4367906465426));
#189342=CARTESIAN_POINT('Ctrl Pts',(20.6971493465552,20.003638991163,14.4382133624897));
#189343=CARTESIAN_POINT('Ctrl Pts',(20.7678866049364,19.8227320909607,14.4501731186814));
#189344=CARTESIAN_POINT('Ctrl Pts',(20.8106148721748,19.6566005100543,14.4613734082948));
#189345=CARTESIAN_POINT('Ctrl Pts',(20.8446793431816,19.3977183482818,14.4786282361314));
#189346=CARTESIAN_POINT('Ctrl Pts',(20.8507199811218,19.3075895787221,14.484583226353));
#189347=CARTESIAN_POINT('Ctrl Pts',(20.8511062726947,19.1787193877652,14.4928166728075));
#189348=CARTESIAN_POINT('Ctrl Pts',(20.8501648825973,19.1400942021931,14.4952476772599));
#189349=CARTESIAN_POINT('Ctrl Pts',(20.8477729843692,19.0939069184367,14.4980939209036));
#189350=CARTESIAN_POINT('Ctrl Pts',(20.8473379908568,19.0863021265278,14.4985605813137));
#189351=CARTESIAN_POINT('Ctrl Pts',(20.8465999732367,19.0745158377066,14.4992805959177));
#189352=CARTESIAN_POINT('Ctrl Pts',(20.8463255634644,19.0703327041752,14.4995355070597));
#189353=CARTESIAN_POINT('Ctrl Pts',(20.8457949434644,19.0625957841527,14.5000057723232));
#189354=CARTESIAN_POINT('Ctrl Pts',(20.8455421895321,19.059041858863,14.5002213121567));
#189355=CARTESIAN_POINT('Ctrl Pts',(20.8449522950971,19.051033238101,14.5007059632867));
#189356=CARTESIAN_POINT('Ctrl Pts',(20.8446100266102,19.0465789748788,14.5009747838381));
#189357=CARTESIAN_POINT('Ctrl Pts',(20.843563909036,19.0335066808487,14.5017616442111));
#189358=CARTESIAN_POINT('Ctrl Pts',(20.8428213482075,19.0248917202775,14.5022775627819));
#189359=CARTESIAN_POINT('Ctrl Pts',(20.8372752150151,18.964849217182,14.5058563574091));
#189360=CARTESIAN_POINT('Ctrl Pts',(20.8306432958255,18.9136035268714,14.5088242564961));
#189361=CARTESIAN_POINT('Ctrl Pts',(20.8185587170377,18.8411644650598,14.5129602940516));
#189362=CARTESIAN_POINT('Ctrl Pts',(20.8146434144928,18.8197374352134,14.5141762363956));
#189363=CARTESIAN_POINT('Ctrl Pts',(20.8014003898098,18.7530964554045,14.517944796383));
#189364=CARTESIAN_POINT('Ctrl Pts',(20.7909238744259,18.7081238241341,14.5204691490588));
#189365=CARTESIAN_POINT('Ctrl Pts',(20.750705117285,18.5578936011013,14.5289363664688));
#189366=CARTESIAN_POINT('Ctrl Pts',(20.7142828992118,18.4546097208712,14.5348247083245));
#189367=CARTESIAN_POINT('Ctrl Pts',(20.6477506747621,18.3042005970275,14.5439696297338));
#189368=CARTESIAN_POINT('Ctrl Pts',(20.6234958178143,18.2546884862718,14.5470774815972));
#189369=CARTESIAN_POINT('Ctrl Pts',(20.5810528677671,18.1759821691211,14.5522219984525));
#189370=CARTESIAN_POINT('Ctrl Pts',(20.5640366496115,18.1461845836009,14.5542192656255));
#189371=CARTESIAN_POINT('Ctrl Pts',(20.5407177317513,18.1075613395594,14.5568800902988));
#189372=CARTESIAN_POINT('Ctrl Pts',(20.5350601991422,18.0983509124228,14.5575201154625));
#189373=CARTESIAN_POINT('Ctrl Pts',(20.5256770208314,18.0833342521811,14.5585728453291));
#189374=CARTESIAN_POINT('Ctrl Pts',(20.5219930462904,18.0775021171327,14.5589840086147));
#189375=CARTESIAN_POINT('Ctrl Pts',(20.5148057898733,18.0662461272976,14.559782079353));
#189376=CARTESIAN_POINT('Ctrl Pts',(20.5113060651028,18.0608200837132,14.5601688513989));
#189377=CARTESIAN_POINT('Ctrl Pts',(20.5031665841553,18.0483263239681,14.5610642185907));
#189378=CARTESIAN_POINT('Ctrl Pts',(20.4985092253758,18.0412702578144,14.5615734698135));
#189379=CARTESIAN_POINT('Ctrl Pts',(20.4858668762618,18.0223639607299,14.5629477367285));
#189380=CARTESIAN_POINT('Ctrl Pts',(20.4778040713471,18.0105665236953,14.5638156802129));
#189381=CARTESIAN_POINT('Ctrl Pts',(20.4027425004075,17.9030891019998,14.5718202668842));
#189382=CARTESIAN_POINT('Ctrl Pts',(20.3280628690436,17.8130414095241,14.5792584531675));
#189383=CARTESIAN_POINT('Ctrl Pts',(20.1325800434948,17.6134714021885,14.5975057709115));
#189384=CARTESIAN_POINT('Ctrl Pts',(20.0058105106286,17.5108171169729,14.6084546176039));
#189385=CARTESIAN_POINT('Ctrl Pts',(19.8409605862959,17.4061746413851,14.6208636027602));
#189386=CARTESIAN_POINT('Ctrl Pts',(19.812975107256,17.3893059244252,14.6229114311541));
#189387=CARTESIAN_POINT('Ctrl Pts',(19.7783138858032,17.3694924436913,14.6253665638587));
#189388=CARTESIAN_POINT('Ctrl Pts',(19.7720005558519,17.3659264454829,14.625810521068));
#189389=CARTESIAN_POINT('Ctrl Pts',(19.7620781584199,17.3603889631995,14.6265030714428));
#189390=CARTESIAN_POINT('Ctrl Pts',(19.7584815252342,17.3583954781264,14.6267530406308));
#189391=CARTESIAN_POINT('Ctrl Pts',(19.7517502412579,17.3546901653239,14.6272188530325));
#189392=CARTESIAN_POINT('Ctrl Pts',(19.7486171013658,17.3529758091606,14.6274348526086));
#189393=CARTESIAN_POINT('Ctrl Pts',(19.7414581821826,17.3490821805475,14.6279265451391));
#189394=CARTESIAN_POINT('Ctrl Pts',(19.7374296714904,17.3469080359281,14.6282019101421));
#189395=CARTESIAN_POINT('Ctrl Pts',(19.7250361550998,17.340271204371,14.6290450983701));
#189396=CARTESIAN_POINT('Ctrl Pts',(19.7166480648367,17.3358515590098,14.6296102594921));
#189397=CARTESIAN_POINT('Ctrl Pts',(19.6008140049927,17.2758098669582,14.6373429789495));
#189398=CARTESIAN_POINT('Ctrl Pts',(19.4888054223823,17.2294337726252,14.6439804904632));
#189399=CARTESIAN_POINT('Ctrl Pts',(19.2028074076327,17.1388164595042,14.6603064442245));
#189400=CARTESIAN_POINT('Ctrl Pts',(19.0260361577631,17.1066157992238,14.6699251213358));
#189401=CARTESIAN_POINT('Ctrl Pts',(18.8258763569788,17.095885544681,14.6815960719128));
#189402=CARTESIAN_POINT('Ctrl Pts',(18.8044107246304,17.0950622164254,14.6828564264813));
#189403=CARTESIAN_POINT('Ctrl Pts',(18.7739144023739,17.0943570711024,14.6846608155752));
#189404=CARTESIAN_POINT('Ctrl Pts',(18.7648908279094,17.0942061505949,14.6851964289294));
#189405=CARTESIAN_POINT('Ctrl Pts',(18.7493378522245,17.0940454940435,14.6861226633269));
#189406=CARTESIAN_POINT('Ctrl Pts',(18.7428088153607,17.0940082585661,14.6865124179165));
#189407=CARTESIAN_POINT('Ctrl Pts',(18.7303180253619,17.0939948074078,14.687259876628));
#189408=CARTESIAN_POINT('Ctrl Pts',(18.724356331665,17.0940135709149,14.6876174195645));
#189409=CARTESIAN_POINT('Ctrl Pts',(18.7088771923133,17.0941276762297,14.6885478454648));
#189410=CARTESIAN_POINT('Ctrl Pts',(18.6993602465038,17.0942620205937,14.6891219453611));
#189411=CARTESIAN_POINT('Ctrl Pts',(18.6670303135265,17.094936489238,14.691079358234));
#189412=CARTESIAN_POINT('Ctrl Pts',(18.6442259007512,17.0957812719165,14.692472157627));
#189413=CARTESIAN_POINT('Ctrl Pts',(18.4439242815153,17.1064462841869,14.704816458693));
#189414=CARTESIAN_POINT('Ctrl Pts',(18.2683373918396,17.1382182293484,14.7164925055961));
#189415=CARTESIAN_POINT('Ctrl Pts',(18.0173335117221,17.2171654974175,14.7338754502794));
#189416=CARTESIAN_POINT('Ctrl Pts',(17.9374624467102,17.2477076936566,14.7395017557208));
#189417=CARTESIAN_POINT('Ctrl Pts',(17.825572944194,17.2984494866377,14.7473429539149));
#189418=CARTESIAN_POINT('Ctrl Pts',(17.7919077578619,17.3148059732196,14.7496960767993));
#189419=CARTESIAN_POINT('Ctrl Pts',(17.7519919166439,17.3355250989737,14.7524633809533));
#189420=CARTESIAN_POINT('Ctrl Pts',(17.7453107263425,17.3390385943472,14.7529257947244));
#189421=CARTESIAN_POINT('Ctrl Pts',(17.734961658416,17.3445518113027,14.7536406786902));
#189422=CARTESIAN_POINT('Ctrl Pts',(17.7312807435796,17.3465267385811,14.7538946712706));
#189423=CARTESIAN_POINT('Ctrl Pts',(17.7244699981977,17.3502069221203,14.7543640863437));
#189424=CARTESIAN_POINT('Ctrl Pts',(17.7213386561767,17.3519091721371,14.7545796891481));
#189425=CARTESIAN_POINT('Ctrl Pts',(17.7142752507894,17.3557720990114,14.755065546715));
#189426=CARTESIAN_POINT('Ctrl Pts',(17.7103457591595,17.3579373661908,14.7553355042486));
#189427=CARTESIAN_POINT('Ctrl Pts',(17.6987856733985,17.3643553108406,14.7561287911656));
#189428=CARTESIAN_POINT('Ctrl Pts',(17.6911743767624,17.3686428045925,14.7566499469768));
#189429=CARTESIAN_POINT('Ctrl Pts',(17.6369037670882,17.3996578786581,14.7603592321784));
#189430=CARTESIAN_POINT('Ctrl Pts',(17.5912470071207,17.4281099125443,14.7634443325496));
#189431=CARTESIAN_POINT('Ctrl Pts',(17.4071720816061,17.5528004539388,14.7759434097013));
#189432=CARTESIAN_POINT('Ctrl Pts',(17.2794066307537,17.6636590734693,14.7848132797346));
#189433=CARTESIAN_POINT('Ctrl Pts',(17.1115465609669,17.8486733009475,14.7986576607972));
#189434=CARTESIAN_POINT('Ctrl Pts',(17.0604711570531,17.9119278994138,14.8032487695533));
#189435=CARTESIAN_POINT('Ctrl Pts',(17.0017259928095,17.9939128590848,14.8091326233095));
#189436=CARTESIAN_POINT('Ctrl Pts',(16.9905152033967,18.0100274481658,14.8102859094099));
#189437=CARTESIAN_POINT('Ctrl Pts',(16.9746597466664,18.0335083332383,14.8119628576744));
#189438=CARTESIAN_POINT('Ctrl Pts',(16.9698336794029,18.0407513332138,14.8124796571692));
#189439=CARTESIAN_POINT('Ctrl Pts',(16.961496440917,18.0534327083962,14.8133837577837));
#189440=CARTESIAN_POINT('Ctrl Pts',(16.9579652719052,18.0588578452648,14.8137703026835));
#189441=CARTESIAN_POINT('Ctrl Pts',(16.9511894775922,18.0693730569864,14.8145191098314));
#189442=CARTESIAN_POINT('Ctrl Pts',(16.9479416282309,18.0744609873468,14.8148812468836));
#189443=CARTESIAN_POINT('Ctrl Pts',(16.9402801642771,18.086577025803,14.815743214593));
#189444=CARTESIAN_POINT('Ctrl Pts',(16.9358860542763,18.0936172951517,14.8162437611199));
#189445=CARTESIAN_POINT('Ctrl Pts',(16.9204544005099,18.1186687376452,14.8180238582751));
#189446=CARTESIAN_POINT('Ctrl Pts',(16.9096454481286,18.1368186156605,14.8193117390215));
#189447=CARTESIAN_POINT('Ctrl Pts',(16.8022349837243,18.3234758268036,14.8325423902071));
#189448=CARTESIAN_POINT('Ctrl Pts',(16.7290069388184,18.504327211604,14.8453728746243));
#189449=CARTESIAN_POINT('Ctrl Pts',(16.663179753398,18.7649447008822,14.8631017335751));
#189450=CARTESIAN_POINT('Ctrl Pts',(16.6487382172893,18.8382445131747,14.8679934987469));
#189451=CARTESIAN_POINT('Ctrl Pts',(16.6333272063734,18.9463232578167,14.8749433520185));
#189452=CARTESIAN_POINT('Ctrl Pts',(16.6292914351499,18.9806043872408,14.8771093030452));
#189453=CARTESIAN_POINT('Ctrl Pts',(16.6254128237953,19.0223111974838,14.8796857602423));
#189454=CARTESIAN_POINT('Ctrl Pts',(16.6247685437036,19.0296549937335,14.8801372244748));
#189455=CARTESIAN_POINT('Ctrl Pts',(16.6238224662587,19.0411267981678,14.8808388654566));
#189456=CARTESIAN_POINT('Ctrl Pts',(16.6234943983557,19.0452524971157,14.881090477006));
#189457=CARTESIAN_POINT('Ctrl Pts',(16.6229060238798,19.0529368627564,14.8815577348391));
#189458=CARTESIAN_POINT('Ctrl Pts',(16.6226426178651,19.0564951893061,14.881773547323));
#189459=CARTESIAN_POINT('Ctrl Pts',(16.6220645668631,19.0645816660428,14.8822627434926));
#189460=CARTESIAN_POINT('Ctrl Pts',(16.621755488347,19.0691101619884,14.8825358122539));
#189461=CARTESIAN_POINT('Ctrl Pts',(16.6209918952302,19.0808538743417,14.8832417451086));
#189462=CARTESIAN_POINT('Ctrl Pts',(16.6205597666355,19.0880705558767,14.8836733851893));
#189463=CARTESIAN_POINT('Ctrl Pts',(16.6180743366903,19.1334751338754,14.8863762693513));
#189464=CARTESIAN_POINT('Ctrl Pts',(16.6170190193779,19.1717131811661,14.8885955101876));
#189465=CARTESIAN_POINT('Ctrl Pts',(16.6169207098274,19.3720991911078,14.9000236634872));
#189466=CARTESIAN_POINT('Ctrl Pts',(16.6354677287759,19.5337233103895,14.9085853062952));
#189467=CARTESIAN_POINT('Ctrl Pts',(16.6916958528464,19.7749057138282,14.9221735840905));
#189468=CARTESIAN_POINT('Ctrl Pts',(16.7161208846119,19.8568711869279,14.9269355617778));
#189469=CARTESIAN_POINT('Ctrl Pts',(16.7454193857226,19.9371102812384,14.9318514580964));
#189470=CARTESIAN_POINT('Origin',(18.734,19.211,0.));
#189471=CARTESIAN_POINT('',(16.7454193622843,19.9371102170485,15.9575278583994));
#189472=CARTESIAN_POINT('',(16.7454193680152,19.9371102327436,15.7328935264317));
#189473=CARTESIAN_POINT('',(16.7454193623258,19.9371102171621,0.));
#189474=CARTESIAN_POINT('',(16.6170004656572,19.2095958660383,15.9109437209775));
#189475=CARTESIAN_POINT('Ctrl Pts',(16.7454193622843,19.9371102170485,15.9575278583994));
#189476=CARTESIAN_POINT('Ctrl Pts',(16.7400022625306,19.9222745358669,15.9565690136276));
#189477=CARTESIAN_POINT('Ctrl Pts',(16.7347514139459,19.9073788646741,15.9556046485865));
#189478=CARTESIAN_POINT('Ctrl Pts',(16.6996561822292,19.8041504797119,15.9489091241404));
#189479=CARTESIAN_POINT('Ctrl Pts',(16.6755129666081,19.714000406954,15.9429927030363));
#189480=CARTESIAN_POINT('Ctrl Pts',(16.6304401550311,19.4865778873416,15.9279421192691));
#189481=CARTESIAN_POINT('Ctrl Pts',(16.6169140878316,19.348289387691,15.9186652721273));
#189482=CARTESIAN_POINT('Ctrl Pts',(16.6170004105495,19.2096815667617,15.9096291409546));
#189483=CARTESIAN_POINT('Ctrl Pts',(16.7454193623258,19.9371102171621,15.155594536163));
#189484=CARTESIAN_POINT('Ctrl Pts',(16.7703664680976,20.005432257441,15.1599719849976));
#189485=CARTESIAN_POINT('Ctrl Pts',(16.7988694131869,20.0725513229361,15.1643494338322));
#189486=CARTESIAN_POINT('Ctrl Pts',(16.8307866970858,20.1380750366667,15.1687268826668));
#189487=CARTESIAN_POINT('Ctrl Pts',(16.8626811573905,20.2035518953247,15.1731012012503));
#189488=CARTESIAN_POINT('Ctrl Pts',(16.8979849019958,20.2674352332271,15.1774755198337));
#189489=CARTESIAN_POINT('Ctrl Pts',(16.9365083970907,20.3293527786304,15.1818498384171));
#189490=CARTESIAN_POINT('Ctrl Pts',(16.9750170528872,20.3912464733181,15.1862224720076));
#189491=CARTESIAN_POINT('Ctrl Pts',(17.0167427428274,20.451175469324,15.190595105598));
#189492=CARTESIAN_POINT('Ctrl Pts',(17.0614509054573,20.5087937148656,15.1949677391885));
#189493=CARTESIAN_POINT('Ctrl Pts',(17.1061565945774,20.566408772638,15.19934013086));
#189494=CARTESIAN_POINT('Ctrl Pts',(17.1538441318443,20.6217129536265,15.2037125225315));
#189495=CARTESIAN_POINT('Ctrl Pts',(17.2042377275192,20.6743920833784,15.2080849142029));
#189496=CARTESIAN_POINT('Ctrl Pts',(17.2546810076,20.7271231509058,15.2124616167334));
#189497=CARTESIAN_POINT('Ctrl Pts',(17.3078353415552,20.7772236475919,15.2168383192638));
#189498=CARTESIAN_POINT('Ctrl Pts',(17.3633875557035,20.8244157949951,15.2212150217942));
#189499=CARTESIAN_POINT('Ctrl Pts',(17.4189660791044,20.8716302923646,15.2255937971092));
#189500=CARTESIAN_POINT('Ctrl Pts',(17.4769443612593,20.9159334030165,15.2299725724242));
#189501=CARTESIAN_POINT('Ctrl Pts',(17.5369777396172,20.9570889748658,15.2343513477392));
#189502=CARTESIAN_POINT('Ctrl Pts',(17.5971222844656,20.9983207563274,15.2387382314282));
#189503=CARTESIAN_POINT('Ctrl Pts',(17.6593291169464,21.0363931003563,15.2431251151172));
#189504=CARTESIAN_POINT('Ctrl Pts',(17.7232266628523,21.0711145827371,15.2475119988062));
#189505=CARTESIAN_POINT('Ctrl Pts',(17.782315602858,21.1032231020898,15.2515687478321));
#189506=CARTESIAN_POINT('Ctrl Pts',(17.8428498211749,21.1324665095571,15.255625496858));
#189507=CARTESIAN_POINT('Ctrl Pts',(17.9045214391031,21.1587305555473,15.2596822458839));
#189508=CARTESIAN_POINT('Ctrl Pts',(17.9712319856141,21.1871405262996,15.2640704548148));
#189509=CARTESIAN_POINT('Ctrl Pts',(18.0395340178846,21.2121746938963,15.2684586637457));
#189510=CARTESIAN_POINT('Ctrl Pts',(18.1090523123261,21.2336540454737,15.2728468726766));
#189511=CARTESIAN_POINT('Ctrl Pts',(18.1784674300924,21.2551015181321,15.2772285687779));
#189512=CARTESIAN_POINT('Ctrl Pts',(18.2490947695204,21.2730045070021,15.2816102648792));
#189513=CARTESIAN_POINT('Ctrl Pts',(18.3205388114184,21.2872318862633,15.2859919609805));
#189514=CARTESIAN_POINT('Ctrl Pts',(18.3918989008814,21.3014425472217,15.2903685082401));
#189515=CARTESIAN_POINT('Ctrl Pts',(18.464073315643,21.3119860848153,15.2947450554998));
#189516=CARTESIAN_POINT('Ctrl Pts',(18.5366526876881,21.31878154426,15.2991216027594));
#189517=CARTESIAN_POINT('Ctrl Pts',(18.6091860309503,21.3255726941232,15.3034953744764));
#189518=CARTESIAN_POINT('Ctrl Pts',(18.6821233428399,21.3286204372107,15.3078691461934));
#189519=CARTESIAN_POINT('Ctrl Pts',(18.7550478100785,21.3278953657871,15.3122429179104));
#189520=CARTESIAN_POINT('Ctrl Pts',(18.8279500861569,21.3271705150052,15.3166153586739));
#189521=CARTESIAN_POINT('Ctrl Pts',(18.90083904328,21.322675133798,15.3209877994375));
#189522=CARTESIAN_POINT('Ctrl Pts',(18.9732972139369,21.3144319203155,15.325360240201));
#189523=CARTESIAN_POINT('Ctrl Pts',(19.0457572373572,21.306188496053,15.3297327927684));
#189524=CARTESIAN_POINT('Ctrl Pts',(19.1177859733815,21.2941971057617,15.3341053453358));
#189525=CARTESIAN_POINT('Ctrl Pts',(19.1889721056855,21.2785321963752,15.3384778979031));
#189526=CARTESIAN_POINT('Ctrl Pts',(19.2602321176427,21.2628510293548,15.3428549884705));
#189527=CARTESIAN_POINT('Ctrl Pts',(19.3306473077957,21.2434888351841,15.3472320790378));
#189528=CARTESIAN_POINT('Ctrl Pts',(19.3998183959355,21.2205708157798,15.3516091696051));
#189529=CARTESIAN_POINT('Ctrl Pts',(19.4690272609739,21.1976402799945,15.3559886506641));
#189530=CARTESIAN_POINT('Ctrl Pts',(19.5369902214647,21.1711502278382,15.360368131723));
#189531=CARTESIAN_POINT('Ctrl Pts',(19.603327519791,21.1412742456278,15.364747612782));
#189532=CARTESIAN_POINT('Ctrl Pts',(19.6697824005332,21.1113453084395,15.3691348564417));
#189533=CARTESIAN_POINT('Ctrl Pts',(19.734605435542,21.0780186771204,15.3735221001015));
#189534=CARTESIAN_POINT('Ctrl Pts',(19.7974415556905,21.0415138780218,15.3779093437612));
#189535=CARTESIAN_POINT('Ctrl Pts',(19.8401640625163,21.0166941322295,15.3808922466959));
#189536=CARTESIAN_POINT('Ctrl Pts',(19.8819686426657,20.9904061565714,15.3838751496307));
#189537=CARTESIAN_POINT('Ctrl Pts',(19.9227521494642,20.9627298099719,15.3868580525654));
#189538=CARTESIAN_POINT('Ctrl Pts',(19.982749592452,20.9220145758598,15.3912462614963));
#189539=CARTESIAN_POINT('Ctrl Pts',(20.0407699602752,20.878133895861,15.3956344704272));
#189540=CARTESIAN_POINT('Ctrl Pts',(20.096459630033,20.8313063773652,15.4000226793581));
#189541=CARTESIAN_POINT('Ctrl Pts',(20.1520666470873,20.7845483586711,15.4044043754594));
#189542=CARTESIAN_POINT('Ctrl Pts',(20.2053494667963,20.7348524915495,15.4087860715606));
#189543=CARTESIAN_POINT('Ctrl Pts',(20.2559837460592,20.6824803691289,15.4131677676619));
#189544=CARTESIAN_POINT('Ctrl Pts',(20.3065585260143,20.63016978812,15.4175443149215));
#189545=CARTESIAN_POINT('Ctrl Pts',(20.3544906143938,20.5751895440799,15.4219208621811));
#189546=CARTESIAN_POINT('Ctrl Pts',(20.3994903578933,20.5178400314363,15.4262974094408));
#189547=CARTESIAN_POINT('Ctrl Pts',(20.4444615632094,20.4605268890201,15.4306711811577));
#189548=CARTESIAN_POINT('Ctrl Pts',(20.4865038163905,20.4008478378294,15.4350449528747));
#189549=CARTESIAN_POINT('Ctrl Pts',(20.5253667770626,20.3391374340196,15.4394187245917));
#189550=CARTESIAN_POINT('Ctrl Pts',(20.5642179116052,20.277445808893,15.4437911653552));
#189551=CARTESIAN_POINT('Ctrl Pts',(20.5998914174618,20.2137244662945,15.4481636061187));
#189552=CARTESIAN_POINT('Ctrl Pts',(20.6321804129385,20.1483367164134,15.4525360468823));
#189553=CARTESIAN_POINT('Ctrl Pts',(20.6644702340484,20.0829472945602,15.4569085994496));
#189554=CARTESIAN_POINT('Ctrl Pts',(20.693375161169,20.0158918142288,15.461281152017));
#189555=CARTESIAN_POINT('Ctrl Pts',(20.718735154665,19.9475564240687,15.4656537045843));
#189556=CARTESIAN_POINT('Ctrl Pts',(20.7441214677188,19.8791501128632,15.4700307951516));
#189557=CARTESIAN_POINT('Ctrl Pts',(20.7659553334551,19.8094616929188,15.4744078857189));
#189558=CARTESIAN_POINT('Ctrl Pts',(20.7841259040681,19.7388946651266,15.4787849762862));
#189559=CARTESIAN_POINT('Ctrl Pts',(20.802306398304,19.6682890980615,15.4831644573452));
#189560=CARTESIAN_POINT('Ctrl Pts',(20.8168195180766,19.5968044408521,15.4875439384041));
#189561=CARTESIAN_POINT('Ctrl Pts',(20.8276056664122,19.5248539685374,15.491923419463));
#189562=CARTESIAN_POINT('Ctrl Pts',(20.8384109331233,19.4527759644936,15.4963106631227));
#189563=CARTESIAN_POINT('Ctrl Pts',(20.8454759896221,19.3802309770758,15.5006979067825));
#189564=CARTESIAN_POINT('Ctrl Pts',(20.8487932306453,19.307636388679,15.5050851504422));
#189565=CARTESIAN_POINT('Ctrl Pts',(20.8510486348925,19.2582790637657,15.5080680533771));
#189566=CARTESIAN_POINT('Ctrl Pts',(20.8515726338748,19.2088988449428,15.511050956312));
#189567=CARTESIAN_POINT('Ctrl Pts',(20.8503765449711,19.1596256883619,15.5140338592469));
#189568=CARTESIAN_POINT('Ctrl Pts',(20.8486169543561,19.0871389496107,15.5184220681777));
#189569=CARTESIAN_POINT('Ctrl Pts',(20.8431255714046,19.0146012223731,15.5228102771086));
#189570=CARTESIAN_POINT('Ctrl Pts',(20.8338948009669,18.9424281755803,15.5271984860395));
#189571=CARTESIAN_POINT('Ctrl Pts',(20.824677730523,18.8703622455555,15.5315801821408));
#189572=CARTESIAN_POINT('Ctrl Pts',(20.8117323505351,18.798660396053,15.5359618782421));
#189573=CARTESIAN_POINT('Ctrl Pts',(20.7951030586573,18.7277369436907,15.5403435743433));
#189574=CARTESIAN_POINT('Ctrl Pts',(20.7784933075209,18.6568968320293,15.544720121603));
#189575=CARTESIAN_POINT('Ctrl Pts',(20.7582083534313,18.5868337678033,15.5490966688626));
#189576=CARTESIAN_POINT('Ctrl Pts',(20.7343439967237,18.5179539014095,15.5534732161222));
#189577=CARTESIAN_POINT('Ctrl Pts',(20.7104947744443,18.4491177176259,15.5578469878392));
#189578=CARTESIAN_POINT('Ctrl Pts',(20.6830708110599,18.3814636975244,15.5622207595562));
#189579=CARTESIAN_POINT('Ctrl Pts',(20.6522179108564,18.3153834266441,15.5665945312732));
#189580=CARTESIAN_POINT('Ctrl Pts',(20.6213743992941,18.2493232642122,15.5709669720367));
#189581=CARTESIAN_POINT('Ctrl Pts',(20.5871042264083,18.1848363370636,15.5753394128002));
#189582=CARTESIAN_POINT('Ctrl Pts',(20.5496008974362,18.1222932528781,15.5797118535638));
#189583=CARTESIAN_POINT('Ctrl Pts',(20.5120966094998,18.0597485694589,15.5840844061311));
#189584=CARTESIAN_POINT('Ctrl Pts',(20.4713592511259,17.9991482403587,15.5884569586985));
#189585=CARTESIAN_POINT('Ctrl Pts',(20.4276268858002,17.940835848524,15.5928295112658));
#189586=CARTESIAN_POINT('Ctrl Pts',(20.3838491333762,17.8824629378895,15.5972066018331));
#189587=CARTESIAN_POINT('Ctrl Pts',(20.3370704580454,17.8263830921189,15.6015836924005));
#189588=CARTESIAN_POINT('Ctrl Pts',(20.2875701403869,17.7729079240542,15.6059607829678));
#189589=CARTESIAN_POINT('Ctrl Pts',(20.2380427887678,17.7194035512154,15.6103402640267));
#189590=CARTESIAN_POINT('Ctrl Pts',(20.1857911812167,17.6685070251039,15.6147197450856));
#189591=CARTESIAN_POINT('Ctrl Pts',(20.1311305579275,17.6204921552834,15.6190992261446));
#189592=CARTESIAN_POINT('Ctrl Pts',(20.0763730490505,17.5723921794284,15.6234864698043));
#189593=CARTESIAN_POINT('Ctrl Pts',(20.0191983762086,17.5271843592176,15.627873713464));
#189594=CARTESIAN_POINT('Ctrl Pts',(19.9599533753588,17.4851010106479,15.6322609571237));
#189595=CARTESIAN_POINT('Ctrl Pts',(19.9196724836152,17.4564883887621,15.6352438600586));
#189596=CARTESIAN_POINT('Ctrl Pts',(19.8784351648856,17.4293192126642,15.6382267629934));
#189597=CARTESIAN_POINT('Ctrl Pts',(19.8363568176098,17.4036543090296,15.6412096659283));
#189598=CARTESIAN_POINT('Ctrl Pts',(19.7744545085684,17.3658981494092,15.6455978748592));
#189599=CARTESIAN_POINT('Ctrl Pts',(19.7104893778663,17.3312522374743,15.6499860837901));
#189600=CARTESIAN_POINT('Ctrl Pts',(19.6448068261832,17.2999479532524,15.654374292721));
#189601=CARTESIAN_POINT('Ctrl Pts',(19.5792217582972,17.2686901297788,15.6587559888222));
#189602=CARTESIAN_POINT('Ctrl Pts',(19.5119247612702,17.2407642944952,15.6631376849235));
#189603=CARTESIAN_POINT('Ctrl Pts',(19.4432882414192,17.2163573777279,15.6675193810248));
#189604=CARTESIAN_POINT('Ctrl Pts',(19.3747323749412,17.1919791410302,15.6718959282844));
#189605=CARTESIAN_POINT('Ctrl Pts',(19.3048405647331,17.1711117694416,15.6762724755441));
#189606=CARTESIAN_POINT('Ctrl Pts',(19.2340061739085,17.1538945515474,15.6806490228037));
#189607=CARTESIAN_POINT('Ctrl Pts',(19.163216705225,17.1366882525625,15.6850227945207));
#189608=CARTESIAN_POINT('Ctrl Pts',(19.0914863095569,17.1231276279116,15.6893965662377));
#189609=CARTESIAN_POINT('Ctrl Pts',(19.0192231694674,17.1133020370895,15.6937703379547));
#189610=CARTESIAN_POINT('Ctrl Pts',(18.9469820192941,17.1034794362276,15.6981427787182));
#189611=CARTESIAN_POINT('Ctrl Pts',(18.8742089242417,17.0973896776779,15.7025152194818));
#189612=CARTESIAN_POINT('Ctrl Pts',(18.8013202474334,17.0950706570668,15.7068876602453));
#189613=CARTESIAN_POINT('Ctrl Pts',(18.7284297068536,17.0927515771582,15.7112602128127));
#189614=CARTESIAN_POINT('Ctrl Pts',(18.6554240608475,17.0942034399582,15.71563276538));
#189615=CARTESIAN_POINT('Ctrl Pts',(18.5827210675495,17.0994120466822,15.7200053179474));
#189616=CARTESIAN_POINT('Ctrl Pts',(18.5099426203428,17.1046260590948,15.7243824085147));
#189617=CARTESIAN_POINT('Ctrl Pts',(18.4374679351488,17.1136045652851,15.7287594990821));
#189618=CARTESIAN_POINT('Ctrl Pts',(18.3657101983343,17.1262814046042,15.7331365896494));
#189619=CARTESIAN_POINT('Ctrl Pts',(18.2939132719564,17.1389651672158,15.7375160707084));
#189620=CARTESIAN_POINT('Ctrl Pts',(18.2228345439091,17.1553511759151,15.7418955517673));
#189621=CARTESIAN_POINT('Ctrl Pts',(18.1528748782421,17.1753225715104,15.7462750328263));
#189622=CARTESIAN_POINT('Ctrl Pts',(18.0827912095374,17.1953293662704,15.750662276486));
#189623=CARTESIAN_POINT('Ctrl Pts',(18.0138310210268,17.2189340823966,15.7550495201457));
#189624=CARTESIAN_POINT('Ctrl Pts',(17.9463773894242,17.2459708339799,15.7594367638054));
#189625=CARTESIAN_POINT('Ctrl Pts',(17.900515419752,17.2643532198009,15.7624196667402));
#189626=CARTESIAN_POINT('Ctrl Pts',(17.8553494637698,17.2843211191871,15.7654025696749));
#189627=CARTESIAN_POINT('Ctrl Pts',(17.8109931300722,17.3058104246385,15.7683854726097));
#189628=CARTESIAN_POINT('Ctrl Pts',(17.7457396290594,17.3374237771892,15.7727736815406));
#189629=CARTESIAN_POINT('Ctrl Pts',(17.6819847879022,17.3724551543895,15.7771618904715));
#189630=CARTESIAN_POINT('Ctrl Pts',(17.6201101194241,17.4107393705492,15.7815500994024));
#189631=CARTESIAN_POINT('Ctrl Pts',(17.558327283213,17.4489667665845,15.7859317955037));
#189632=CARTESIAN_POINT('Ctrl Pts',(17.4984194869966,17.4904371661199,15.790313491605));
#189633=CARTESIAN_POINT('Ctrl Pts',(17.4407454860727,17.5349386162175,15.7946951877062));
#189634=CARTESIAN_POINT('Ctrl Pts',(17.3831392566899,17.5793877735698,15.7990717349659));
#189635=CARTESIAN_POINT('Ctrl Pts',(17.3277619882545,17.626860612876,15.8034482822255));
#189636=CARTESIAN_POINT('Ctrl Pts',(17.2749437204164,17.6771017722784,15.8078248294852));
#189637=CARTESIAN_POINT('Ctrl Pts',(17.2221589491561,17.7273110694676,15.8121986012021));
#189638=CARTESIAN_POINT('Ctrl Pts',(17.1719303071395,17.7802848717172,15.8165723729191));
#189639=CARTESIAN_POINT('Ctrl Pts',(17.12455387304,17.8357283306876,15.8209461446361));
#189640=CARTESIAN_POINT('Ctrl Pts',(17.0771918557485,17.8911549180272,15.8253185853996));
#189641=CARTESIAN_POINT('Ctrl Pts',(17.0326806364324,17.9490493035727,15.8296910261632));
#189642=CARTESIAN_POINT('Ctrl Pts',(16.9912774487782,18.0090819040121,15.8340634669268));
#189643=CARTESIAN_POINT('Ctrl Pts',(16.94987320244,18.0691160394918,15.8384360194941));
#189644=CARTESIAN_POINT('Ctrl Pts',(16.911577417771,18.1312881001858,15.8428085720615));
#189645=CARTESIAN_POINT('Ctrl Pts',(16.8766042803952,18.1952391320819,15.8471811246288));
#189646=CARTESIAN_POINT('Ctrl Pts',(16.8415948465783,18.259256534771,15.8515582151961));
#189647=CARTESIAN_POINT('Ctrl Pts',(16.8099151769005,18.3250561707614,15.8559353057635));
#189648=CARTESIAN_POINT('Ctrl Pts',(16.7817332906699,18.3922548042025,15.8603123963308));
#189649=CARTESIAN_POINT('Ctrl Pts',(16.7535360132653,18.4594901373113,15.8646918773897));
#189650=CARTESIAN_POINT('Ctrl Pts',(16.728840486062,18.5281255348702,15.8690713584487));
#189651=CARTESIAN_POINT('Ctrl Pts',(16.7077654290803,18.5977606799873,15.8734508395076));
#189652=CARTESIAN_POINT('Ctrl Pts',(16.6866530167015,18.6675192529316,15.8778380831674));
#189653=CARTESIAN_POINT('Ctrl Pts',(16.6691740053289,18.7382806434227,15.8822253268271));
#189654=CARTESIAN_POINT('Ctrl Pts',(16.6553962633245,18.8096329536713,15.8866125704868));
#189655=CARTESIAN_POINT('Ctrl Pts',(16.6460287263817,18.8581456491476,15.8895954734216));
#189656=CARTESIAN_POINT('Ctrl Pts',(16.6383710944437,18.9069313156785,15.8925783763564));
#189657=CARTESIAN_POINT('Ctrl Pts',(16.6324309574258,18.9558597262409,15.8955612792912));
#189658=CARTESIAN_POINT('Ctrl Pts',(16.6222201199426,19.0399655384572,15.9006887598533));
#189659=CARTESIAN_POINT('Ctrl Pts',(16.617056776629,19.1246963446803,15.9058162404154));
#189660=CARTESIAN_POINT('Ctrl Pts',(16.6170004656572,19.2095958660383,15.9109437209775));
#189661=CARTESIAN_POINT('',(16.6170004208928,19.2096650617603,15.6876313494247));
#189662=CARTESIAN_POINT('Ctrl Pts',(16.7454193857226,19.9371102812384,14.9318514580964));
#189663=CARTESIAN_POINT('Ctrl Pts',(16.7539898736387,19.9605820686035,14.9332894712505));
#189664=CARTESIAN_POINT('Ctrl Pts',(16.7629773978124,19.9839061466847,14.9347402980908));
#189665=CARTESIAN_POINT('Ctrl Pts',(16.7777126708588,20.0202157393077,14.9370362397452));
#189666=CARTESIAN_POINT('Ctrl Pts',(16.7831788110021,20.0333058438738,14.9378716807806));
#189667=CARTESIAN_POINT('Ctrl Pts',(16.7921001472685,20.054080620314,14.9392103641091));
#189668=CARTESIAN_POINT('Ctrl Pts',(16.7954704382653,20.061801448952,14.939710719563));
#189669=CARTESIAN_POINT('Ctrl Pts',(16.8015031078453,20.0753994382038,14.9405970664953));
#189670=CARTESIAN_POINT('Ctrl Pts',(16.8041464536429,20.0812849620356,14.9409824018903));
#189671=CARTESIAN_POINT('Ctrl Pts',(16.8096767348222,20.0934492779395,14.9417823977819));
#189672=CARTESIAN_POINT('Ctrl Pts',(16.8125675897148,20.0997261940465,14.9421971898744));
#189673=CARTESIAN_POINT('Ctrl Pts',(16.8200827103448,20.115835715273,14.9432669169788));
#189674=CARTESIAN_POINT('Ctrl Pts',(16.8247519941562,20.1256469857614,14.9439234049188));
#189675=CARTESIAN_POINT('Ctrl Pts',(16.8446948433191,20.1667334551882,14.9466939028832));
#189676=CARTESIAN_POINT('Ctrl Pts',(16.8606622632928,20.197664031381,14.9488319850111));
#189677=CARTESIAN_POINT('Ctrl Pts',(16.9043949234205,20.277486977492,14.9544918295384));
#189678=CARTESIAN_POINT('Ctrl Pts',(16.9333566765409,20.3256891777366,14.9580538176853));
#189679=CARTESIAN_POINT('Ctrl Pts',(17.0332351059343,20.4778524387781,14.9697636317365));
#189680=CARTESIAN_POINT('Ctrl Pts',(17.1115039702421,20.5766567273707,14.9781230611111));
#189681=CARTESIAN_POINT('Ctrl Pts',(17.2668972841675,20.7404771510173,14.9930005545619));
#189682=CARTESIAN_POINT('Ctrl Pts',(17.3407870119797,20.8080764090406,14.9995201489052));
#189683=CARTESIAN_POINT('Ctrl Pts',(17.4267853807552,20.8762245834316,15.0062995441743));
#189684=CARTESIAN_POINT('Ctrl Pts',(17.4344245245433,20.8821931563487,15.0068951758941));
#189685=CARTESIAN_POINT('Ctrl Pts',(17.4457640317482,20.8909281020863,15.0077693341156));
#189686=CARTESIAN_POINT('Ctrl Pts',(17.4494327578418,20.8937350770054,15.0080506260364));
#189687=CARTESIAN_POINT('Ctrl Pts',(17.4559575636312,20.898693489956,15.0085481520704));
#189688=CARTESIAN_POINT('Ctrl Pts',(17.458809932896,20.9008497207262,15.008764721023));
#189689=CARTESIAN_POINT('Ctrl Pts',(17.4649328356837,20.9054539594798,15.0092276133082));
#189690=CARTESIAN_POINT('Ctrl Pts',(17.4682049867575,20.9078997240385,15.0094737804235));
#189691=CARTESIAN_POINT('Ctrl Pts',(17.4772061298521,20.9145870918971,15.0101476987871));
#189692=CARTESIAN_POINT('Ctrl Pts',(17.4829495581171,20.9188093005004,15.0105741179115));
#189693=CARTESIAN_POINT('Ctrl Pts',(17.5137221088844,20.9411928062782,15.0128403498042));
#189694=CARTESIAN_POINT('Ctrl Pts',(17.5391269884115,20.9588340858544,15.0146464277926));
#189695=CARTESIAN_POINT('Ctrl Pts',(17.6171834034302,21.0105391244381,15.0200319022));
#189696=CARTESIAN_POINT('Ctrl Pts',(17.6709725473431,21.0428280908763,15.023524549167));
#189697=CARTESIAN_POINT('Ctrl Pts',(17.8443350941308,21.136683329717,15.0343589198719));
#189698=CARTESIAN_POINT('Ctrl Pts',(17.9683762767184,21.1892772672582,15.04152766775));
#189699=CARTESIAN_POINT('Ctrl Pts',(18.1354764561819,21.2420399640214,15.0512527113468));
#189700=CARTESIAN_POINT('Ctrl Pts',(18.1747299578942,21.2531974787995,15.0535399438182));
#189701=CARTESIAN_POINT('Ctrl Pts',(18.2613894662419,21.2751438718862,15.0586206858394));
#189702=CARTESIAN_POINT('Ctrl Pts',(18.3088928173713,21.2854478761445,15.0614259934544));
#189703=CARTESIAN_POINT('Ctrl Pts',(18.3691073316157,21.2963539688809,15.0650250123058));
#189704=CARTESIAN_POINT('Ctrl Pts',(18.3815281411256,21.2984892606516,15.0657696568682));
#189705=CARTESIAN_POINT('Ctrl Pts',(18.4012400691229,21.3016970430008,15.0669552633267));
#189706=CARTESIAN_POINT('Ctrl Pts',(18.4085191187147,21.3028426066562,15.0673939024762));
#189707=CARTESIAN_POINT('Ctrl Pts',(18.4220931020484,21.3049062908642,15.0682134788143));
#189708=CARTESIAN_POINT('Ctrl Pts',(18.4283864970922,21.3058340873165,15.068594104358));
#189709=CARTESIAN_POINT('Ctrl Pts',(18.4423736161947,21.3078317504683,15.0694415085676));
#189710=CARTESIAN_POINT('Ctrl Pts',(18.4500692117576,21.3088876620265,15.0699087235272));
#189711=CARTESIAN_POINT('Ctrl Pts',(18.4724466382034,21.311832683153,15.0712702336299));
#189712=CARTESIAN_POINT('Ctrl Pts',(18.4871424637311,21.3136101547827,15.0721680370904));
#189713=CARTESIAN_POINT('Ctrl Pts',(18.6040634136054,21.32650918205,15.0793414021644));
#189714=CARTESIAN_POINT('Ctrl Pts',(18.7069418250766,21.3303218337858,15.0858477838725));
#189715=CARTESIAN_POINT('Ctrl Pts',(18.9653686792341,21.3210777729614,15.1026338937291));
#189716=CARTESIAN_POINT('Ctrl Pts',(19.1199578148917,21.2983410167675,15.1131041132348));
#189717=CARTESIAN_POINT('Ctrl Pts',(19.3214647071208,21.2455352974122,15.1265600164924));
#189718=CARTESIAN_POINT('Ctrl Pts',(19.3717727891725,21.23033046406,15.1298978690499));
#189719=CARTESIAN_POINT('Ctrl Pts',(19.4296851277199,21.2104465982146,15.1336748223086));
#189720=CARTESIAN_POINT('Ctrl Pts',(19.4378857914466,21.2075743899462,15.1342080934621));
#189721=CARTESIAN_POINT('Ctrl Pts',(19.4502843215203,21.2031460311206,15.1350117180827));
#189722=CARTESIAN_POINT('Ctrl Pts',(19.4544952029299,21.2016269620328,15.1352841903171));
#189723=CARTESIAN_POINT('Ctrl Pts',(19.4620494559043,21.1988746660993,15.1357721316086));
#189724=CARTESIAN_POINT('Ctrl Pts',(19.4653945446348,21.1976463497611,15.1359878864854));
#189725=CARTESIAN_POINT('Ctrl Pts',(19.4726614168395,21.1949571127201,15.1364559143958));
#189726=CARTESIAN_POINT('Ctrl Pts',(19.4765819620693,21.1934930123824,15.1367079945564));
#189727=CARTESIAN_POINT('Ctrl Pts',(19.487595220487,21.1893429338197,15.1374149877408));
#189728=CARTESIAN_POINT('Ctrl Pts',(19.4946779612244,21.1866304217608,15.1378683428083));
#189729=CARTESIAN_POINT('Ctrl Pts',(19.5371983230854,21.1700836251916,15.1405829221296));
#189730=CARTESIAN_POINT('Ctrl Pts',(19.5722747614423,21.1553333116667,15.1427926142434));
#189731=CARTESIAN_POINT('Ctrl Pts',(19.6869971843577,21.1034080159472,15.1499806697728));
#189732=CARTESIAN_POINT('Ctrl Pts',(19.7647300507507,21.0622184479534,15.1547896859524));
#189733=CARTESIAN_POINT('Ctrl Pts',(19.9882626701981,20.92531359813,15.1690493690483));
#189734=CARTESIAN_POINT('Ctrl Pts',(20.125023331932,20.816332767206,15.1784223776321));
#189735=CARTESIAN_POINT('Ctrl Pts',(20.2630319137663,20.6753371457652,15.1898859646073));
#189736=CARTESIAN_POINT('Ctrl Pts',(20.2789076745533,20.6585780066204,15.1912382687377));
#189737=CARTESIAN_POINT('Ctrl Pts',(20.3009669061003,20.6345150635208,15.1931673763937));
#189738=CARTESIAN_POINT('Ctrl Pts',(20.307380136793,20.6274234400316,15.1937344036085));
#189739=CARTESIAN_POINT('Ctrl Pts',(20.3177190131074,20.6158340556644,15.1946587534172));
#189740=CARTESIAN_POINT('Ctrl Pts',(20.3216741063834,20.6113626556104,15.1950148344409));
#189741=CARTESIAN_POINT('Ctrl Pts',(20.3299107455761,20.6019710392164,15.1957616244884));
#189742=CARTESIAN_POINT('Ctrl Pts',(20.3341885655729,20.597047651748,15.1961524829716));
#189743=CARTESIAN_POINT('Ctrl Pts',(20.3443064345426,20.5852936186386,15.197084160035));
#189744=CARTESIAN_POINT('Ctrl Pts',(20.3501258388067,20.5784454404505,15.1976258215036));
#189745=CARTESIAN_POINT('Ctrl Pts',(20.3695622142201,20.555275662687,15.1994547299663));
#189746=CARTESIAN_POINT('Ctrl Pts',(20.3829765865681,20.5387864960595,15.2007501660214));
#189747=CARTESIAN_POINT('Ctrl Pts',(20.454518435157,20.4480896022527,15.2078448730744));
#189748=CARTESIAN_POINT('Ctrl Pts',(20.5078810015306,20.3702741060108,15.2138291960127));
#189749=CARTESIAN_POINT('Ctrl Pts',(20.6403913997157,20.1463601339531,15.2307281643116));
#189750=CARTESIAN_POINT('Ctrl Pts',(20.7078162184791,19.9941173521913,15.2419109618191));
#189751=CARTESIAN_POINT('Ctrl Pts',(20.769161392288,19.7954406617657,15.2552398611737));
#189752=CARTESIAN_POINT('Ctrl Pts',(20.7803558264263,19.7549495886665,15.2578907564886));
#189753=CARTESIAN_POINT('Ctrl Pts',(20.7921065681289,19.7069250637058,15.2609373336602));
#189754=CARTESIAN_POINT('Ctrl Pts',(20.7938361641377,19.6996914110497,15.2613936398139));
#189755=CARTESIAN_POINT('Ctrl Pts',(20.7965741884452,19.6879673933345,15.2621288605418));
#189756=CARTESIAN_POINT('Ctrl Pts',(20.7976061421072,19.6834826645766,15.2624090751273));
#189757=CARTESIAN_POINT('Ctrl Pts',(20.7994135281255,19.6755091282627,15.2629054123269));
#189758=CARTESIAN_POINT('Ctrl Pts',(20.8001947567421,19.6720216917714,15.2631218638132));
#189759=CARTESIAN_POINT('Ctrl Pts',(20.8018524605339,19.6645327779747,15.2635853007269));
#189760=CARTESIAN_POINT('Ctrl Pts',(20.8027261520414,19.6605307417158,15.2638321257698));
#189761=CARTESIAN_POINT('Ctrl Pts',(20.8050989832853,19.649508305544,15.2645097039309));
#189762=CARTESIAN_POINT('Ctrl Pts',(20.8065740551022,19.6424827019394,15.2649391007146));
#189763=CARTESIAN_POINT('Ctrl Pts',(20.8143549231348,19.6044625841117,15.2672500886656));
#189764=CARTESIAN_POINT('Ctrl Pts',(20.820001603532,19.573335429299,15.2690963467679));
#189765=CARTESIAN_POINT('Ctrl Pts',(20.8505127867128,19.3806475842458,15.2803089196882));
#189766=CARTESIAN_POINT('Ctrl Pts',(20.8572959239024,19.2167691245175,15.288947077949));
#189767=CARTESIAN_POINT('Ctrl Pts',(20.8364521815894,18.9369715422696,15.3043057683836));
#189768=CARTESIAN_POINT('Ctrl Pts',(20.8180851646639,18.8211532181488,15.310841028377));
#189769=CARTESIAN_POINT('Ctrl Pts',(20.7868423565605,18.6935721747176,15.3185359664359));
#189770=CARTESIAN_POINT('Ctrl Pts',(20.7833021632317,18.6797242485116,15.3193776654132));
#189771=CARTESIAN_POINT('Ctrl Pts',(20.7774449090729,18.6577429152904,15.3207244938376));
#189772=CARTESIAN_POINT('Ctrl Pts',(20.7752188323004,18.6495855597734,15.321226680366));
#189773=CARTESIAN_POINT('Ctrl Pts',(20.7712067809272,18.6352229386219,15.322115157907));
#189774=CARTESIAN_POINT('Ctrl Pts',(20.7694411641,18.6290120630748,15.3225007825789));
#189775=CARTESIAN_POINT('Ctrl Pts',(20.7657306820127,18.616183208605,15.3233002847032));
#189776=CARTESIAN_POINT('Ctrl Pts',(20.7637818325093,18.6095664706549,15.3237142883545));
#189777=CARTESIAN_POINT('Ctrl Pts',(20.7586966804201,18.5926076104067,15.3247796723959));
#189778=CARTESIAN_POINT('Ctrl Pts',(20.755513485927,18.5822798598391,15.3254325815888));
#189779=CARTESIAN_POINT('Ctrl Pts',(20.7419000500467,18.5392840059105,15.3281681890784));
#189780=CARTESIAN_POINT('Ctrl Pts',(20.7307563660389,18.5068488895757,15.3302742090506));
#189781=CARTESIAN_POINT('Ctrl Pts',(20.6996742249987,18.423061317881,15.3358289974504));
#189782=CARTESIAN_POINT('Ctrl Pts',(20.6785116348424,18.3721935814454,15.3393161566803));
#189783=CARTESIAN_POINT('Ctrl Pts',(20.6094731207301,18.2229453871187,15.3498858340951));
#189784=CARTESIAN_POINT('Ctrl Pts',(20.5559342397031,18.1273932888991,15.3571167426616));
#189785=CARTESIAN_POINT('Ctrl Pts',(20.4696765519122,17.9980523862437,15.3673864045986));
#189786=CARTESIAN_POINT('Ctrl Pts',(20.4428468031232,17.9605369627796,15.3704265358808));
#189787=CARTESIAN_POINT('Ctrl Pts',(20.4015473515862,17.9066032387941,15.3748628240414));
#189788=CARTESIAN_POINT('Ctrl Pts',(20.3880145265824,17.8894853114626,15.3762810190783));
#189789=CARTESIAN_POINT('Ctrl Pts',(20.341525361071,17.8325133753209,15.381028265932));
#189790=CARTESIAN_POINT('Ctrl Pts',(20.3073714259154,17.7936551332002,15.3843123525774));
#189791=CARTESIAN_POINT('Ctrl Pts',(20.2658813749311,17.7498007449412,15.3880359783541));
#189792=CARTESIAN_POINT('Ctrl Pts',(20.2598985665197,17.743554130336,15.3885667909802));
#189793=CARTESIAN_POINT('Ctrl Pts',(20.2507673947793,17.7341365559843,15.3893674523829));
#189794=CARTESIAN_POINT('Ctrl Pts',(20.2476470837842,17.730938694265,15.3896393970778));
#189795=CARTESIAN_POINT('Ctrl Pts',(20.2420203055254,17.7252084760256,15.3901267768547));
#189796=CARTESIAN_POINT('Ctrl Pts',(20.2395175609509,17.7226725599414,15.390342494809));
#189797=CARTESIAN_POINT('Ctrl Pts',(20.2340564916344,17.7171669799952,15.3908108837112));
#189798=CARTESIAN_POINT('Ctrl Pts',(20.2310957553338,17.7141997896139,15.39106335939));
#189799=CARTESIAN_POINT('Ctrl Pts',(20.2227314692954,17.7058669160822,15.3917725814064));
#189800=CARTESIAN_POINT('Ctrl Pts',(20.2173076902002,17.7005215035763,15.3922277539953));
#189801=CARTESIAN_POINT('Ctrl Pts',(20.1842244208549,17.6682662906918,15.3949765676913));
#189802=CARTESIAN_POINT('Ctrl Pts',(20.1558603352602,17.6420857964822,15.3972171535982));
#189803=CARTESIAN_POINT('Ctrl Pts',(20.058954150256,17.5574280457007,15.4045581070713));
#189804=CARTESIAN_POINT('Ctrl Pts',(19.9873946456709,17.5025480256279,15.4094808085603));
#189805=CARTESIAN_POINT('Ctrl Pts',(19.7703833223275,17.3571155107752,15.4236858801083));
#189806=CARTESIAN_POINT('Ctrl Pts',(19.6172056334296,17.2794412940434,15.4329071361176));
#189807=CARTESIAN_POINT('Ctrl Pts',(19.4344668967409,17.2131067737044,15.4442004797186));
#189808=CARTESIAN_POINT('Ctrl Pts',(19.4124499011301,17.2055232772403,15.4455644100353));
#189809=CARTESIAN_POINT('Ctrl Pts',(19.3811909321228,17.1953301470797,15.4475072852567));
#189810=CARTESIAN_POINT('Ctrl Pts',(19.3720489474315,17.1924176770146,15.448076261037));
#189811=CARTESIAN_POINT('Ctrl Pts',(19.3571816673791,17.1877923195441,15.4490029225743));
#189812=CARTESIAN_POINT('Ctrl Pts',(19.3514682969361,17.1860413312947,15.4493593542314));
#189813=CARTESIAN_POINT('Ctrl Pts',(19.3395085480022,17.1824313245277,15.4501061785426));
#189814=CARTESIAN_POINT('Ctrl Pts',(19.3332608536926,17.1805769158699,15.4504967175602));
#189815=CARTESIAN_POINT('Ctrl Pts',(19.3184050357965,17.176242027617,15.4514263448715));
#189816=CARTESIAN_POINT('Ctrl Pts',(19.3097895856061,17.1737872960114,15.4519662662143));
#189817=CARTESIAN_POINT('Ctrl Pts',(19.2808414063668,17.1657376214908,15.4537832258321));
#189818=CARTESIAN_POINT('Ctrl Pts',(19.2604412156062,17.1603919641542,15.4550683081813));
#189819=CARTESIAN_POINT('Ctrl Pts',(19.1497846573137,17.1331556070415,15.462066148723));
#189820=CARTESIAN_POINT('Ctrl Pts',(19.058253163731,17.116920214522,15.467958349142));
#189821=CARTESIAN_POINT('Ctrl Pts',(18.8138470815258,17.0899782168669,15.4839174380439));
#189822=CARTESIAN_POINT('Ctrl Pts',(18.6603742072936,17.0897540284929,15.4941950117233));
#189823=CARTESIAN_POINT('Ctrl Pts',(18.5049138745307,17.1064288737145,15.5043133508622));
#189824=CARTESIAN_POINT('Ctrl Pts',(18.5016052520021,17.1067916548598,15.5045285402374));
#189825=CARTESIAN_POINT('Ctrl Pts',(18.4463215744407,17.112985336748,15.508121378768));
#189826=CARTESIAN_POINT('Ctrl Pts',(18.3945744225895,17.1207331115901,15.511444043667));
#189827=CARTESIAN_POINT('Ctrl Pts',(18.3346378583765,17.1319920334928,15.51520572589));
#189828=CARTESIAN_POINT('Ctrl Pts',(18.3261223376977,17.1336458983902,15.5157380987637));
#189829=CARTESIAN_POINT('Ctrl Pts',(18.3132311110595,17.1362319279637,15.5165406408463));
#189830=CARTESIAN_POINT('Ctrl Pts',(18.3088479175262,17.1371256744297,15.5168129204609));
#189831=CARTESIAN_POINT('Ctrl Pts',(18.3009783792444,17.1387562949975,15.5173006565556));
#189832=CARTESIAN_POINT('Ctrl Pts',(18.2974910493845,17.1394880802724,15.5175163977796));
#189833=CARTESIAN_POINT('Ctrl Pts',(18.2899095596507,17.141098984263,15.5179845567174));
#189834=CARTESIAN_POINT('Ctrl Pts',(18.2858161685686,17.1419814432685,15.5182367806863));
#189835=CARTESIAN_POINT('Ctrl Pts',(18.2743053499205,17.1444987252268,15.5189445839966));
#189836=CARTESIAN_POINT('Ctrl Pts',(18.266893976798,17.1461613484341,15.5193985996502));
#189837=CARTESIAN_POINT('Ctrl Pts',(18.2222245625897,17.1564350344067,15.5221255551546));
#189838=CARTESIAN_POINT('Ctrl Pts',(18.1851939538965,17.1660150045352,15.5243464149621));
#189839=CARTESIAN_POINT('Ctrl Pts',(18.0632300955745,17.2011196280644,15.5315894552164));
#189840=CARTESIAN_POINT('Ctrl Pts',(17.9796374669179,17.2309770110101,15.5364393202617));
#189841=CARTESIAN_POINT('Ctrl Pts',(17.7391841251487,17.3343086564626,15.5506743656102));
#189842=CARTESIAN_POINT('Ctrl Pts',(17.5892041011794,17.4218480817856,15.5599880976046));
#189843=CARTESIAN_POINT('Ctrl Pts',(17.4330760379047,17.54072306789,15.5713882879402));
#189844=CARTESIAN_POINT('Ctrl Pts',(17.4148345318103,17.5550922157579,15.5727484584683));
#189845=CARTESIAN_POINT('Ctrl Pts',(17.3894034723066,17.5758116226648,15.5746868797984));
#189846=CARTESIAN_POINT('Ctrl Pts',(17.3820146505983,17.5819154527558,15.5752552240178));
#189847=CARTESIAN_POINT('Ctrl Pts',(17.3700880593261,17.5919049121813,15.5761811361066));
#189848=CARTESIAN_POINT('Ctrl Pts',(17.3655247904159,17.5957599915372,15.5765374539416));
#189849=CARTESIAN_POINT('Ctrl Pts',(17.3563677345484,17.6035625901537,15.5772566518401));
#189850=CARTESIAN_POINT('Ctrl Pts',(17.3517744515964,17.6075106119641,15.5776195507566));
#189851=CARTESIAN_POINT('Ctrl Pts',(17.3407774267729,17.617045145513,15.5784935872025));
#189852=CARTESIAN_POINT('Ctrl Pts',(17.3343902949704,17.6226505778043,15.5790055088681));
#189853=CARTESIAN_POINT('Ctrl Pts',(17.3141082723577,17.640667679329,15.5806449335358));
#189854=CARTESIAN_POINT('Ctrl Pts',(17.3003436997171,17.6532241196501,15.5817785065278));
#189855=CARTESIAN_POINT('Ctrl Pts',(17.2684821235173,17.6830691533946,15.5844528387181));
#189856=CARTESIAN_POINT('Ctrl Pts',(17.2505227223724,17.7004999497849,15.5859995790608));
#189857=CARTESIAN_POINT('Ctrl Pts',(17.1883845743239,17.7629864006987,15.5914930531436));
#189858=CARTESIAN_POINT('Ctrl Pts',(17.1459183158394,17.8096913987636,15.5955093279175));
#189859=CARTESIAN_POINT('Ctrl Pts',(17.0460725584953,17.9298797406588,15.6056137560596));
#189860=CARTESIAN_POINT('Ctrl Pts',(16.9913396084864,18.0053877006036,15.6117696252287));
#189861=CARTESIAN_POINT('Ctrl Pts',(16.8765795697267,18.1879280743259,15.6260161984534));
#189862=CARTESIAN_POINT('Ctrl Pts',(16.8205102116619,18.2970795750735,15.6340842561212));
#189863=CARTESIAN_POINT('Ctrl Pts',(16.7706161806151,18.419228364474,15.6422329730794));
#189864=CARTESIAN_POINT('Ctrl Pts',(16.7671004762423,18.4280027994263,15.6428135690498));
#189865=CARTESIAN_POINT('Ctrl Pts',(16.761971558019,18.441056023011,15.6436699308315));
#189866=CARTESIAN_POINT('Ctrl Pts',(16.7603133023376,18.4453168252728,15.6439483053232));
#189867=CARTESIAN_POINT('Ctrl Pts',(16.7573844801105,18.4529150190147,15.6444426227967));
#189868=CARTESIAN_POINT('Ctrl Pts',(16.7561085443978,18.4562502783246,15.6446588844482));
#189869=CARTESIAN_POINT('Ctrl Pts',(16.7533801307651,18.4634367090344,15.6451233012706));
#189870=CARTESIAN_POINT('Ctrl Pts',(16.7519304471216,18.4672888809334,15.645371288754));
#189871=CARTESIAN_POINT('Ctrl Pts',(16.7479520099501,18.477954842668,15.6460553443868));
#189872=CARTESIAN_POINT('Ctrl Pts',(16.7454470684721,18.4847775385847,15.6464900128808));
#189873=CARTESIAN_POINT('Ctrl Pts',(16.7317893099674,18.522577654256,15.6488829192696));
#189874=CARTESIAN_POINT('Ctrl Pts',(16.7213245088896,18.553800934464,15.6508027967598));
#189875=CARTESIAN_POINT('Ctrl Pts',(16.663602434638,18.7403594717851,15.6620105295621));
#189876=CARTESIAN_POINT('Ctrl Pts',(16.6336097086608,18.9004828368032,15.6705926721185));
#189877=CARTESIAN_POINT('Ctrl Pts',(16.6187709866018,19.1114653678293,15.6821718417595));
#189878=CARTESIAN_POINT('Ctrl Pts',(16.6170313866306,19.1605583302494,15.6848817035565));
#189879=CARTESIAN_POINT('Ctrl Pts',(16.6170004208928,19.2096650617603,15.6876313494247));
#189880=CARTESIAN_POINT('Ctrl Pts',(16.6170004192075,19.2096677371557,15.6876314992289));
#189881=CARTESIAN_POINT('Ctrl Pts',(16.6169565169163,19.2794295956352,15.6915376949309));
#189882=CARTESIAN_POINT('Ctrl Pts',(16.6203608902705,19.3491464384918,15.695521234486));
#189883=CARTESIAN_POINT('Ctrl Pts',(16.6282125593119,19.4288414159146,15.7002202367451));
#189884=CARTESIAN_POINT('Ctrl Pts',(16.6293001579621,19.4391100548907,15.7008284403706));
#189885=CARTESIAN_POINT('Ctrl Pts',(16.6312632478519,19.4564336662004,15.7018593105948));
#189886=CARTESIAN_POINT('Ctrl Pts',(16.6320992368905,19.4634929969452,15.7022807376865));
#189887=CARTESIAN_POINT('Ctrl Pts',(16.6337047673432,19.4764896969377,15.7030591573664));
#189888=CARTESIAN_POINT('Ctrl Pts',(16.634463973354,19.4824282873715,15.7034158213631));
#189889=CARTESIAN_POINT('Ctrl Pts',(16.6360832813492,19.4946812512276,15.7041537772539));
#189890=CARTESIAN_POINT('Ctrl Pts',(16.636946723945,19.5009951149655,15.704535171221));
#189891=CARTESIAN_POINT('Ctrl Pts',(16.6389488848926,19.5151590790055,15.7053933371429));
#189892=CARTESIAN_POINT('Ctrl Pts',(16.6401032381611,19.5230068402183,15.7058705994675));
#189893=CARTESIAN_POINT('Ctrl Pts',(16.6431522418392,19.5429558410351,15.7070884172785));
#189894=CARTESIAN_POINT('Ctrl Pts',(16.6451078426903,19.5550473418584,15.7078308944189));
#189895=CARTESIAN_POINT('Ctrl Pts',(16.6571525015344,19.6256277823438,15.7121907880401));
#189896=CARTESIAN_POINT('Ctrl Pts',(16.6695919117635,19.6836836981216,15.7158823675275));
#189897=CARTESIAN_POINT('Ctrl Pts',(16.6997698751888,19.8003540239869,15.7235211230514));
#189898=CARTESIAN_POINT('Ctrl Pts',(16.717645350903,19.8588760239831,15.7274691388482));
#189899=CARTESIAN_POINT('Ctrl Pts',(16.7404566866214,19.9234094087007,15.7319399174074));
#189900=CARTESIAN_POINT('Ctrl Pts',(16.742920533714,19.9302667353381,15.7324164742522));
#189901=CARTESIAN_POINT('Ctrl Pts',(16.7454193680152,19.9371102327436,15.7328935264317));
#189902=CARTESIAN_POINT('Origin',(18.734,19.211,0.));
#189903=CARTESIAN_POINT('',(16.745419290545,19.9371100205779,16.7554728823802));
#189904=CARTESIAN_POINT('',(16.7454193623258,19.9371102171621,16.5356516081066));
#189905=CARTESIAN_POINT('',(16.7454193623258,19.9371102171621,0.));
#189906=CARTESIAN_POINT('Ctrl Pts',(16.745419290545,19.9371100205779,16.7554728823802));
#189907=CARTESIAN_POINT('Ctrl Pts',(16.7246695916352,19.8802833003706,16.7521869364102));
#189908=CARTESIAN_POINT('Ctrl Pts',(16.7063536245855,19.8225613881497,16.7488940155909));
#189909=CARTESIAN_POINT('Ctrl Pts',(16.6648838496181,19.6693480707068,16.740135080757));
#189910=CARTESIAN_POINT('Ctrl Pts',(16.6458617517716,19.5729388012687,16.7345998747667));
#189911=CARTESIAN_POINT('Ctrl Pts',(16.6317631857905,19.4610092327402,16.7279812613245));
#189912=CARTESIAN_POINT('Ctrl Pts',(16.630081116969,19.4464348251301,16.727115924452));
#189913=CARTESIAN_POINT('Ctrl Pts',(16.6277432520215,19.4241464784128,16.725786761891));
#189914=CARTESIAN_POINT('Ctrl Pts',(16.6269780369723,19.4164442857521,16.7253263840921));
#189915=CARTESIAN_POINT('Ctrl Pts',(16.6257184973999,19.4030185094664,16.7245219869061));
#189916=CARTESIAN_POINT('Ctrl Pts',(16.625205197247,19.3972967553643,16.7241785687105));
#189917=CARTESIAN_POINT('Ctrl Pts',(16.6241033853661,19.3844264219209,16.7234047089429));
#189918=CARTESIAN_POINT('Ctrl Pts',(16.6235279049358,19.3772768241441,16.7229738616919));
#189919=CARTESIAN_POINT('Ctrl Pts',(16.6220830309171,19.3581085306041,16.7218161096034));
#189920=CARTESIAN_POINT('Ctrl Pts',(16.621279911401,19.3460852393745,16.7210871332558));
#189921=CARTESIAN_POINT('Ctrl Pts',(16.618172337624,19.292714307176,16.717838498664));
#189922=CARTESIAN_POINT('Ctrl Pts',(16.6169788916403,19.2513134328802,16.7152843270478));
#189923=CARTESIAN_POINT('Ctrl Pts',(16.6170878341668,19.0404276598584,16.7020917041995));
#189924=CARTESIAN_POINT('Ctrl Pts',(16.6375272230776,18.8715947971973,16.6908605299796));
#189925=CARTESIAN_POINT('Ctrl Pts',(16.702560257478,18.6062621558145,16.672847566007));
#189926=CARTESIAN_POINT('Ctrl Pts',(16.7346397979375,18.507423998555,16.666071013703));
#189927=CARTESIAN_POINT('Ctrl Pts',(16.7775028812636,18.4023580070007,16.6590602237326));
#189928=CARTESIAN_POINT('Ctrl Pts',(16.7812238447903,18.3934132191032,16.6584649950007));
#189929=CARTESIAN_POINT('Ctrl Pts',(16.7868091126874,18.3802425294775,16.657591313127));
#189930=CARTESIAN_POINT('Ctrl Pts',(16.7886259927346,18.3759968268016,16.657310098822));
#189931=CARTESIAN_POINT('Ctrl Pts',(16.7918742110363,18.3684745083349,16.6568126585519));
#189932=CARTESIAN_POINT('Ctrl Pts',(16.7932999703368,18.365195542807,16.6565960981773));
#189933=CARTESIAN_POINT('Ctrl Pts',(16.7963728345764,18.3581772384418,16.6561331672323));
#189934=CARTESIAN_POINT('Ctrl Pts',(16.7980224551061,18.3544390616336,16.6558869531772));
#189935=CARTESIAN_POINT('Ctrl Pts',(16.8025810939232,18.3441892523944,16.655212773983));
#189936=CARTESIAN_POINT('Ctrl Pts',(16.8055122412708,18.3376874381741,16.6547861426865));
#189937=CARTESIAN_POINT('Ctrl Pts',(16.8213484150772,18.3030284875306,16.652516757392));
#189938=CARTESIAN_POINT('Ctrl Pts',(16.8348380844036,18.2751407161349,16.6507078494936));
#189939=CARTESIAN_POINT('Ctrl Pts',(16.9233519990827,18.1019550748452,16.6395211976233));
#189940=CARTESIAN_POINT('Ctrl Pts',(17.0143947981724,17.9654490679667,16.6308786786183));
#189941=CARTESIAN_POINT('Ctrl Pts',(17.1964661805042,17.7510195854767,16.6154835399497));
#189942=CARTESIAN_POINT('Ctrl Pts',(17.2800216307166,17.6677908082219,16.6089132926449));
#189943=CARTESIAN_POINT('Ctrl Pts',(17.3809923290847,17.5827298217725,16.6011789747488));
#189944=CARTESIAN_POINT('Ctrl Pts',(17.3920227710195,17.5736269109291,16.6003367972576));
#189945=CARTESIAN_POINT('Ctrl Pts',(17.4097221145588,17.5593194556075,16.5989893461463));
#189946=CARTESIAN_POINT('Ctrl Pts',(17.4163315615324,17.5540418165527,16.5984870197534));
#189947=CARTESIAN_POINT('Ctrl Pts',(17.4280424984634,17.5448050228377,16.5975983792116));
#189948=CARTESIAN_POINT('Ctrl Pts',(17.4331308376923,17.5408293144498,16.5972127321872));
#189949=CARTESIAN_POINT('Ctrl Pts',(17.443691252499,17.5326556067532,16.5964132666152));
#189950=CARTESIAN_POINT('Ctrl Pts',(17.4491658064831,17.5284609485545,16.595999322277));
#189951=CARTESIAN_POINT('Ctrl Pts',(17.4632677550172,17.5177648534525,16.5949342653797));
#189952=CARTESIAN_POINT('Ctrl Pts',(17.4719245154293,17.5113026256377,16.5942816258302));
#189953=CARTESIAN_POINT('Ctrl Pts',(17.5082358350089,17.4846267580573,16.5915486303661));
#189954=CARTESIAN_POINT('Ctrl Pts',(17.536328225208,17.4650204860326,16.5894450084457));
#189955=CARTESIAN_POINT('Ctrl Pts',(17.6107288256385,17.4157353769852,16.5838980506992));
#189956=CARTESIAN_POINT('Ctrl Pts',(17.6577375167945,17.3871657287952,16.5804164588884));
#189957=CARTESIAN_POINT('Ctrl Pts',(17.801346532386,17.3073736054511,16.5698574783396));
#189958=CARTESIAN_POINT('Ctrl Pts',(17.9008524439255,17.261769992505,16.5626316640186));
#189959=CARTESIAN_POINT('Ctrl Pts',(18.039394298169,17.2108298469172,16.5528807495674));
#189960=CARTESIAN_POINT('Ctrl Pts',(18.0757169552015,17.1985832302097,16.5503529715578));
#189961=CARTESIAN_POINT('Ctrl Pts',(18.1433448553178,17.177808749775,16.5457180079641));
#189962=CARTESIAN_POINT('Ctrl Pts',(18.1745528341501,17.169001182349,16.5436066233097));
#189963=CARTESIAN_POINT('Ctrl Pts',(18.212137643054,17.1593203262083,16.5411051345695));
#189964=CARTESIAN_POINT('Ctrl Pts',(18.2183307334069,17.1577550042924,16.5406942824693));
#189965=CARTESIAN_POINT('Ctrl Pts',(18.2666531635486,17.1457737901268,16.5374993986305));
#189966=CARTESIAN_POINT('Ctrl Pts',(18.309090097105,17.13662671331,16.5347576356891));
#189967=CARTESIAN_POINT('Ctrl Pts',(18.3591675801458,17.1274342940059,16.5316198059652));
#189968=CARTESIAN_POINT('Ctrl Pts',(18.3665610632222,17.1261177429526,16.5311590135902));
#189969=CARTESIAN_POINT('Ctrl Pts',(18.3785177425675,17.124054207189,16.5304179989488));
#189970=CARTESIAN_POINT('Ctrl Pts',(18.3830765787805,17.1232827943285,16.5301364438628));
#189971=CARTESIAN_POINT('Ctrl Pts',(18.3911658570303,17.1219412313611,16.5296386267069));
#189972=CARTESIAN_POINT('Ctrl Pts',(18.3946952499603,17.1213650855483,16.5294220283407));
#189973=CARTESIAN_POINT('Ctrl Pts',(18.4022569537474,17.1201503598322,16.5289592658243));
#189974=CARTESIAN_POINT('Ctrl Pts',(18.4062896456748,17.1195145014028,16.5287132568855));
#189975=CARTESIAN_POINT('Ctrl Pts',(18.4173566531271,17.117802295488,16.5280402178807));
#189976=CARTESIAN_POINT('Ctrl Pts',(18.4243946703043,17.116749732627,16.5276145141493));
#189977=CARTESIAN_POINT('Ctrl Pts',(18.4618791162159,17.1113368816409,16.5253588792002));
#189978=CARTESIAN_POINT('Ctrl Pts',(18.492414256584,17.1076047593987,16.523562310079));
#189979=CARTESIAN_POINT('Ctrl Pts',(18.584888629601,17.0983427349107,16.5182155740101));
#189980=CARTESIAN_POINT('Ctrl Pts',(18.6470032789016,17.0948743852522,16.514750696061));
#189981=CARTESIAN_POINT('Ctrl Pts',(18.8561893653951,17.0924221438487,16.5032496679188));
#189982=CARTESIAN_POINT('Ctrl Pts',(19.0029705058823,17.1060159321909,16.4954296952454));
#189983=CARTESIAN_POINT('Ctrl Pts',(19.2201483498836,17.1492320882218,16.4830634215144));
#189984=CARTESIAN_POINT('Ctrl Pts',(19.2923125597153,17.1675929203147,16.4788225186518));
#189985=CARTESIAN_POINT('Ctrl Pts',(19.3758670947347,17.1936087766758,16.473687661536));
#189986=CARTESIAN_POINT('Ctrl Pts',(19.3883419999393,17.1976204404449,16.4729150804174));
#189987=CARTESIAN_POINT('Ctrl Pts',(19.4085551339427,17.2043282518725,16.4716532531572));
#189988=CARTESIAN_POINT('Ctrl Pts',(19.4163164830941,17.2069540056485,16.4711663272382));
#189989=CARTESIAN_POINT('Ctrl Pts',(19.4301121917377,17.2117106840662,16.4702964330498));
#189990=CARTESIAN_POINT('Ctrl Pts',(19.4361525305248,17.2138240501195,16.4699140507445));
#189991=CARTESIAN_POINT('Ctrl Pts',(19.4488620289639,17.218335575704,16.4691062592796));
#189992=CARTESIAN_POINT('Ctrl Pts',(19.4555289026579,17.2207398991496,16.4686806487239));
#189993=CARTESIAN_POINT('Ctrl Pts',(19.4731358310597,17.2271897083577,16.46755159351));
#189994=CARTESIAN_POINT('Ctrl Pts',(19.484054625507,17.2312921679688,16.4668462527708));
#189995=CARTESIAN_POINT('Ctrl Pts',(19.534679482511,17.2507921006258,16.4635514427574));
#189996=CARTESIAN_POINT('Ctrl Pts',(19.5739467578328,17.2672943445876,16.4609250660654));
#189997=CARTESIAN_POINT('Ctrl Pts',(19.6808049399562,17.3160448259265,16.4535752855994));
#189998=CARTESIAN_POINT('Ctrl Pts',(19.747219281087,17.3507098368175,16.4487751085701));
#189999=CARTESIAN_POINT('Ctrl Pts',(19.9505280367823,17.4709481445123,16.4333851190777));
#190000=CARTESIAN_POINT('Ctrl Pts',(20.0795525272035,17.5686822305257,16.4225220026474));
#190001=CARTESIAN_POINT('Ctrl Pts',(20.224495956478,17.7071251808197,16.4097036822652));
#190002=CARTESIAN_POINT('Ctrl Pts',(20.2520178616942,17.7349106104409,16.4072404220939));
#190003=CARTESIAN_POINT('Ctrl Pts',(20.2837411157461,17.7687640199376,16.4043825205715));
#190004=CARTESIAN_POINT('Ctrl Pts',(20.2886986039635,17.774109467504,16.4039353497376));
#190005=CARTESIAN_POINT('Ctrl Pts',(20.2967102016839,17.7828380359052,16.4032119417372));
#190006=CARTESIAN_POINT('Ctrl Pts',(20.2997811254766,17.7862055453039,16.4029344702753));
#190007=CARTESIAN_POINT('Ctrl Pts',(20.3052379551506,17.7922283373583,16.402441138735));
#190008=CARTESIAN_POINT('Ctrl Pts',(20.3076280367449,17.7948797561537,16.4022249649996));
#190009=CARTESIAN_POINT('Ctrl Pts',(20.3127661517649,17.8006087562576,16.4017600432424));
#190010=CARTESIAN_POINT('Ctrl Pts',(20.3155118899632,17.8036883198961,16.4015114665818));
#190011=CARTESIAN_POINT('Ctrl Pts',(20.3230995124472,17.8122486919477,16.4008241221562));
#190012=CARTESIAN_POINT('Ctrl Pts',(20.3279220797709,17.817746652829,16.4003867762728));
#190013=CARTESIAN_POINT('Ctrl Pts',(20.3547444705111,17.848647026923,16.3979508884506));
#190014=CARTESIAN_POINT('Ctrl Pts',(20.3761668454562,17.8745470077442,16.3959923481967));
#190015=CARTESIAN_POINT('Ctrl Pts',(20.4412124468213,17.9571151169236,16.3899642859086));
#190016=CARTESIAN_POINT('Ctrl Pts',(20.482589594342,18.0154927328052,16.3860076714569));
#190017=CARTESIAN_POINT('Ctrl Pts',(20.5429465993985,18.1105063385437,16.3798505009514));
#190018=CARTESIAN_POINT('Ctrl Pts',(20.5639455136523,18.145789414133,16.3776214270986));
#190019=CARTESIAN_POINT('Ctrl Pts',(20.6583766843838,18.3154990533026,16.3670747101152));
#190020=CARTESIAN_POINT('Ctrl Pts',(20.7180951192703,18.4570057854318,16.3587457285326));
#190021=CARTESIAN_POINT('Ctrl Pts',(20.7689033717466,18.626678043596,16.3484638515463));
#190022=CARTESIAN_POINT('Ctrl Pts',(20.7753904899178,18.6497614768637,16.3470600861361));
#190023=CARTESIAN_POINT('Ctrl Pts',(20.7839518867568,18.6823407995586,16.345069942165));
#190024=CARTESIAN_POINT('Ctrl Pts',(20.7863551308774,18.6917489044613,16.344494206495));
#190025=CARTESIAN_POINT('Ctrl Pts',(20.7901377398609,18.7069934945601,16.3435595128754));
#190026=CARTESIAN_POINT('Ctrl Pts',(20.7915571947188,18.7128199601271,16.3432018528114));
#190027=CARTESIAN_POINT('Ctrl Pts',(20.7944636216607,18.7249743655636,16.3424548386266));
#190028=CARTESIAN_POINT('Ctrl Pts',(20.7959462411955,18.7313032723961,16.3420653486577));
#190029=CARTESIAN_POINT('Ctrl Pts',(20.799381494115,18.7462776736658,16.3411425467131));
#190030=CARTESIAN_POINT('Ctrl Pts',(20.8013090161772,18.7549287503857,16.3406084343721));
#190031=CARTESIAN_POINT('Ctrl Pts',(20.8075221734102,18.7836634661622,16.3388309615162));
#190032=CARTESIAN_POINT('Ctrl Pts',(20.8115698005841,18.8037968641545,16.337580026374));
#190033=CARTESIAN_POINT('Ctrl Pts',(20.8314782480676,18.910862404558,16.3308965939813));
#190034=CARTESIAN_POINT('Ctrl Pts',(20.8421754222857,18.9986546603401,16.3253022103307));
#190035=CARTESIAN_POINT('Ctrl Pts',(20.8550353117621,19.2175624178871,16.3111031703415));
#190036=CARTESIAN_POINT('Ctrl Pts',(20.8505699181128,19.3487024208538,16.3023645922308));
#190037=CARTESIAN_POINT('Ctrl Pts',(20.8292590227255,19.5159566727771,16.2913124790122));
#190038=CARTESIAN_POINT('Ctrl Pts',(20.8234988295758,19.5532043442221,16.2888590613911));
#190039=CARTESIAN_POINT('Ctrl Pts',(20.8085427384265,19.635333049971,16.2834921737488));
#190040=CARTESIAN_POINT('Ctrl Pts',(20.7988778753951,19.6801120962688,16.2805945839741));
#190041=CARTESIAN_POINT('Ctrl Pts',(20.7859168049057,19.7319458812973,16.2773008926848));
#190042=CARTESIAN_POINT('Ctrl Pts',(20.7840263901472,19.7393360570858,16.2768327487511));
#190043=CARTESIAN_POINT('Ctrl Pts',(20.780929639554,19.7511752458745,16.2760852869147));
#190044=CARTESIAN_POINT('Ctrl Pts',(20.7797486660075,19.7556307391212,16.2758045640693));
#190045=CARTESIAN_POINT('Ctrl Pts',(20.7776237389928,19.7635430784875,16.2753071022196));
#190046=CARTESIAN_POINT('Ctrl Pts',(20.7766855502521,19.767001424159,16.2750900338363));
#190047=CARTESIAN_POINT('Ctrl Pts',(20.7746697822938,19.7743579643213,16.2746290758649));
#190048=CARTESIAN_POINT('Ctrl Pts',(20.7735898148796,19.7782554486306,16.2743853269422));
#190049=CARTESIAN_POINT('Ctrl Pts',(20.7706253378867,19.7888360036352,16.273724825518));
#190050=CARTESIAN_POINT('Ctrl Pts',(20.7687190874887,19.7955130041981,16.2733093180115));
#190051=CARTESIAN_POINT('Ctrl Pts',(20.758825701485,19.8295315033812,16.2711984871581));
#190052=CARTESIAN_POINT('Ctrl Pts',(20.7503197718666,19.8567206049526,16.2695316531591));
#190053=CARTESIAN_POINT('Ctrl Pts',(20.7236962125246,19.93615886539,16.2646990407753));
#190054=CARTESIAN_POINT('Ctrl Pts',(20.7040766411596,19.9878817649128,16.2616004195423));
#190055=CARTESIAN_POINT('Ctrl Pts',(20.6279151111834,20.1671529447908,16.250841529363));
#190056=CARTESIAN_POINT('Ctrl Pts',(20.5608244880492,20.2898220633271,16.2434223354561));
#190057=CARTESIAN_POINT('Ctrl Pts',(20.4312369283178,20.4795527097187,16.2307030373898));
#190058=CARTESIAN_POINT('Ctrl Pts',(20.375608594012,20.5507602502537,16.2255976687706));
#190059=CARTESIAN_POINT('Ctrl Pts',(20.306488425148,20.6284475178536,16.2195012888534));
#190060=CARTESIAN_POINT('Ctrl Pts',(20.2972674636175,20.6386106391665,16.2186927337745));
#190061=CARTESIAN_POINT('Ctrl Pts',(20.2823192451956,20.6547677183842,16.2173890926125));
#190062=CARTESIAN_POINT('Ctrl Pts',(20.2766543597056,20.660819034635,16.2168966581788));
#190063=CARTESIAN_POINT('Ctrl Pts',(20.2665317263132,20.6715056876137,16.2160194686251));
#190064=CARTESIAN_POINT('Ctrl Pts',(20.2620880977403,20.6761542989883,16.2156353254261));
#190065=CARTESIAN_POINT('Ctrl Pts',(20.2527842164345,20.6857989986069,16.2148329003311));
#190066=CARTESIAN_POINT('Ctrl Pts',(20.2479203387233,20.6907914679354,16.2144144625062));
#190067=CARTESIAN_POINT('Ctrl Pts',(20.2352221115373,20.7036972798069,16.2133247026955));
#190068=CARTESIAN_POINT('Ctrl Pts',(20.2273498981579,20.7115729144436,16.2126517147788));
#190069=CARTESIAN_POINT('Ctrl Pts',(20.1928651768653,20.745532497253,16.2097145428775));
#190070=CARTESIAN_POINT('Ctrl Pts',(20.1656300313635,20.7709720401183,16.2074225248212));
#190071=CARTESIAN_POINT('Ctrl Pts',(20.0914624691273,20.8366711127104,16.2012486613143));
#190072=CARTESIAN_POINT('Ctrl Pts',(20.0434163015008,20.8756136910291,16.1973168952285));
#190073=CARTESIAN_POINT('Ctrl Pts',(19.8779264279346,20.9981448460856,16.1840130226358));
#190074=CARTESIAN_POINT('Ctrl Pts',(19.7536638110197,21.0718425637511,16.1743708179557));
#190075=CARTESIAN_POINT('Ctrl Pts',(19.5561730937709,21.1632103471318,16.1601534545917));
#190076=CARTESIAN_POINT('Ctrl Pts',(19.4878797777643,21.190586187392,16.1554258374913));
#190077=CARTESIAN_POINT('Ctrl Pts',(19.4093591050794,21.2174067927065,16.15030157305));
#190078=CARTESIAN_POINT('Ctrl Pts',(19.4004041024093,21.2203988450572,16.1497216563738));
#190079=CARTESIAN_POINT('Ctrl Pts',(19.3870852358878,21.2247501231999,16.1488660996675));
#190080=CARTESIAN_POINT('Ctrl Pts',(19.3827366467357,21.2261552416896,16.1485878579399));
#190081=CARTESIAN_POINT('Ctrl Pts',(19.3749821542232,21.2286331748907,16.1480936856081));
#190082=CARTESIAN_POINT('Ctrl Pts',(19.3715780610609,21.2297114620852,16.1478774370711));
#190083=CARTESIAN_POINT('Ctrl Pts',(19.3642429340592,21.232014546315,16.1474129469189));
#190084=CARTESIAN_POINT('Ctrl Pts',(19.3603110623449,21.2332364862193,16.1471648735279));
#190085=CARTESIAN_POINT('Ctrl Pts',(19.3494226399989,21.2365855675942,16.1464803387246));
#190086=CARTESIAN_POINT('Ctrl Pts',(19.3424585761159,21.238688359219,16.1460452801959));
#190087=CARTESIAN_POINT('Ctrl Pts',(19.3038226743174,21.2501374563907,16.1436461723351));
#190088=CARTESIAN_POINT('Ctrl Pts',(19.2719444579931,21.2587781812171,16.1417207179608));
#190089=CARTESIAN_POINT('Ctrl Pts',(19.0823016222497,21.3054469577167,16.1305132437402));
#190090=CARTESIAN_POINT('Ctrl Pts',(18.9207760926261,21.3259818990315,16.121935265882));
#190091=CARTESIAN_POINT('Ctrl Pts',(18.6417834485212,21.3292077687061,16.1066601224681));
#190092=CARTESIAN_POINT('Ctrl Pts',(18.5251943999455,21.3209059261457,16.1001448248109));
#190093=CARTESIAN_POINT('Ctrl Pts',(18.3957719800454,21.300855248428,16.0924723578614));
#190094=CARTESIAN_POINT('Ctrl Pts',(18.3816749903978,21.2985249041794,16.0916309482477));
#190095=CARTESIAN_POINT('Ctrl Pts',(18.3592762883116,21.2945888782798,16.0902844963049));
#190096=CARTESIAN_POINT('Ctrl Pts',(18.3509585881051,21.2930758265259,16.0897823942899));
#190097=CARTESIAN_POINT('Ctrl Pts',(18.3363047984326,21.290319411796,16.0888940151354));
#190098=CARTESIAN_POINT('Ctrl Pts',(18.3299648808633,21.2890968001274,16.0885084038623));
#190099=CARTESIAN_POINT('Ctrl Pts',(18.3168631743454,21.2865079995885,16.0877088792968));
#190100=CARTESIAN_POINT('Ctrl Pts',(18.3101022792114,21.2851377264375,16.0872948395577));
#190101=CARTESIAN_POINT('Ctrl Pts',(18.2927644340792,21.2815354448603,16.086229256861));
#190102=CARTESIAN_POINT('Ctrl Pts',(18.2821977599815,21.2792554441323,16.0855761840006));
#190103=CARTESIAN_POINT('Ctrl Pts',(18.2381616067095,21.2694000759662,16.0828389909618));
#190104=CARTESIAN_POINT('Ctrl Pts',(18.2048628859242,21.261092749854,16.0807315152868));
#190105=CARTESIAN_POINT('Ctrl Pts',(18.1186329480229,21.2373394554466,16.0751719718688));
#190106=CARTESIAN_POINT('Ctrl Pts',(18.0660798099717,21.2206293178599,16.0716814313361));
#190107=CARTESIAN_POINT('Ctrl Pts',(17.8183605189002,21.1310723495553,16.0547497765255));
#190108=CARTESIAN_POINT('Ctrl Pts',(17.6340286963579,21.0317481243175,16.0405613082684));
#190109=CARTESIAN_POINT('Ctrl Pts',(17.4635472504763,20.9044164569456,16.0271469099946));
#190110=CARTESIAN_POINT('Ctrl Pts',(17.459929650207,20.9016963742497,16.0268621739342));
#190111=CARTESIAN_POINT('Ctrl Pts',(17.4399644348665,20.8865840077796,16.0252904001417));
#190112=CARTESIAN_POINT('Ctrl Pts',(17.423788203183,20.8739657033604,16.0240156419576));
#190113=CARTESIAN_POINT('Ctrl Pts',(17.4027742875478,20.8570767388507,16.0223607681787));
#190114=CARTESIAN_POINT('Ctrl Pts',(17.3977696868257,20.8530167722384,16.021966734501));
#190115=CARTESIAN_POINT('Ctrl Pts',(17.3897405835027,20.8464421696548,16.021334815623));
#190116=CARTESIAN_POINT('Ctrl Pts',(17.3867044593084,20.8439418837618,16.021095919218));
#190117=CARTESIAN_POINT('Ctrl Pts',(17.3810330768478,20.8392448448374,16.0206498049985));
#190118=CARTESIAN_POINT('Ctrl Pts',(17.37839619008,20.8370501469915,16.0204424447824));
#190119=CARTESIAN_POINT('Ctrl Pts',(17.3721594728651,20.8318335722181,16.0199521149872));
#190120=CARTESIAN_POINT('Ctrl Pts',(17.3685643265438,20.8288060800984,16.0196695545674));
#190121=CARTESIAN_POINT('Ctrl Pts',(17.3573283055216,20.8192800310532,16.0187866327351));
#190122=CARTESIAN_POINT('Ctrl Pts',(17.3497233865365,20.8127390171248,16.0181892933377));
#190123=CARTESIAN_POINT('Ctrl Pts',(17.3318906562942,20.7971791580403,16.0167884017336));
#190124=CARTESIAN_POINT('Ctrl Pts',(17.3217028098532,20.7881149609138,16.0159879186903));
#190125=CARTESIAN_POINT('Ctrl Pts',(17.2862676036678,20.7559692647704,16.0132001988145));
#190126=CARTESIAN_POINT('Ctrl Pts',(17.2614916193388,20.7323738661735,16.0112447046715));
#190127=CARTESIAN_POINT('Ctrl Pts',(17.1836200343751,20.6545274682123,16.0050355499663));
#190128=CARTESIAN_POINT('Ctrl Pts',(17.1328642362608,20.5980166581805,16.0008885283496));
#190129=CARTESIAN_POINT('Ctrl Pts',(16.9773509795776,20.4049278997275,15.987405588632));
#190130=CARTESIAN_POINT('Ctrl Pts',(16.8861939356731,20.2583230267282,15.97814116619));
#190131=CARTESIAN_POINT('Ctrl Pts',(16.8039965162978,20.0812386346228,15.9667992733134));
#190132=CARTESIAN_POINT('Ctrl Pts',(16.7945630666716,20.0600070948626,15.9654384283983));
#190133=CARTESIAN_POINT('Ctrl Pts',(16.7817336785057,20.0298022341832,15.9634992082359));
#190134=CARTESIAN_POINT('Ctrl Pts',(16.7780461753215,20.0209540233104,15.9629307507748));
#190135=CARTESIAN_POINT('Ctrl Pts',(16.7721583255951,20.0065513397011,15.9620047042708));
#190136=CARTESIAN_POINT('Ctrl Pts',(16.7699211488636,20.0010119966965,15.9616483659906));
#190137=CARTESIAN_POINT('Ctrl Pts',(16.7652920189449,19.9894088744396,15.9609015515739));
#190138=CARTESIAN_POINT('Ctrl Pts',(16.7629045691137,19.9833433765759,15.9605109282529));
#190139=CARTESIAN_POINT('Ctrl Pts',(16.7572999093651,19.968909057057,15.9595807591194));
#190140=CARTESIAN_POINT('Ctrl Pts',(16.7541077963288,19.9605306832021,15.9590403776587));
#190141=CARTESIAN_POINT('Ctrl Pts',(16.7491001803603,19.9471319197495,15.9581753838691));
#190142=CARTESIAN_POINT('Ctrl Pts',(16.747250275411,19.9421244949192,15.9578519361455));
#190143=CARTESIAN_POINT('Ctrl Pts',(16.7454193622843,19.9371102170485,15.9575278583994));
#190144=CARTESIAN_POINT('Ctrl Pts',(16.7454193680152,19.9371102327436,15.7328935264317));
#190145=CARTESIAN_POINT('Ctrl Pts',(16.798649296165,20.0828897568259,15.7430556461159));
#190146=CARTESIAN_POINT('Ctrl Pts',(16.8677537179851,20.2223914641028,15.7534874284883));
#190147=CARTESIAN_POINT('Ctrl Pts',(16.9691681762378,20.3806708068013,15.7654348636817));
#190148=CARTESIAN_POINT('Ctrl Pts',(16.9874716141485,20.4078291582142,15.7674874434137));
#190149=CARTESIAN_POINT('Ctrl Pts',(17.0105924212788,20.4404746693608,15.7699474701984));
#190150=CARTESIAN_POINT('Ctrl Pts',(17.0148164431233,20.4463742535236,15.7703917390174));
#190151=CARTESIAN_POINT('Ctrl Pts',(17.021482460663,20.4555841055966,15.7710846669077));
#190152=CARTESIAN_POINT('Ctrl Pts',(17.0239038680462,20.4589091066991,15.7713347044207));
#190153=CARTESIAN_POINT('Ctrl Pts',(17.0284457977148,20.4651078972136,15.7718005762138));
#190154=CARTESIAN_POINT('Ctrl Pts',(17.0305638780919,20.4679833465874,15.7720165672672));
#190155=CARTESIAN_POINT('Ctrl Pts',(17.0354125296699,20.4745309832887,15.7725081525716));
#190156=CARTESIAN_POINT('Ctrl Pts',(17.0381477316739,20.4781996784281,15.7727834194274));
#190157=CARTESIAN_POINT('Ctrl Pts',(17.0465812782217,20.4894352878942,15.7736260085721));
#190158=CARTESIAN_POINT('Ctrl Pts',(17.0523186213081,20.4969729686298,15.7741906742504));
#190159=CARTESIAN_POINT('Ctrl Pts',(17.1322494728731,20.6005357757961,15.7819443090162));
#190160=CARTESIAN_POINT('Ctrl Pts',(17.2145265084586,20.6900616502173,15.7886000137398));
#190161=CARTESIAN_POINT('Ctrl Pts',(17.3839409567636,20.8452498537013,15.8011016927523));
#190162=CARTESIAN_POINT('Ctrl Pts',(17.4693494968485,20.9122025499698,15.8069416369717));
#190163=CARTESIAN_POINT('Ctrl Pts',(17.6043723453465,21.0022394222406,15.8159742098848));
#190164=CARTESIAN_POINT('Ctrl Pts',(17.65036458098,21.0304314974606,15.8190177901784));
#190165=CARTESIAN_POINT('Ctrl Pts',(17.7169499389581,21.0678257620917,15.8234133557038));
#190166=CARTESIAN_POINT('Ctrl Pts',(17.7366921729607,21.0785036228313,15.8247152238287));
#190167=CARTESIAN_POINT('Ctrl Pts',(17.7717692385924,21.0967606971742,15.8270282161289));
#190168=CARTESIAN_POINT('Ctrl Pts',(17.7870333157027,21.1044718161461,15.8280346940689));
#190169=CARTESIAN_POINT('Ctrl Pts',(17.8097462614675,21.1156026250584,15.8295329803547));
#190170=CARTESIAN_POINT('Ctrl Pts',(17.8171244995112,21.1191654661722,15.8300197929981));
#190171=CARTESIAN_POINT('Ctrl Pts',(17.8300551778246,21.1253171859167,15.8308732028732));
#190172=CARTESIAN_POINT('Ctrl Pts',(17.8355985519317,21.1279249768118,15.8312391387822));
#190173=CARTESIAN_POINT('Ctrl Pts',(17.8466658480813,21.1330728571377,15.8319699184297));
#190174=CARTESIAN_POINT('Ctrl Pts',(17.8521895491263,21.135613283971,15.832334746131));
#190175=CARTESIAN_POINT('Ctrl Pts',(17.86543084042,21.1416341676935,15.8332095647526));
#190176=CARTESIAN_POINT('Ctrl Pts',(17.8731584706618,21.1450921727126,15.8337203218163));
#190177=CARTESIAN_POINT('Ctrl Pts',(17.9011809216221,21.1574306108246,15.8355733565837));
#190178=CARTESIAN_POINT('Ctrl Pts',(17.9215935298959,21.1660384673653,15.8369248828483));
#190179=CARTESIAN_POINT('Ctrl Pts',(18.113850674268,21.2435811101518,15.8496743496089));
#190180=CARTESIAN_POINT('Ctrl Pts',(18.2938780018495,21.2899988859761,15.861867295555));
#190181=CARTESIAN_POINT('Ctrl Pts',(18.5574473246742,21.3221582929071,15.8793984992523));
#190182=CARTESIAN_POINT('Ctrl Pts',(18.6377947894787,21.3273427106033,15.8846846200392));
#190183=CARTESIAN_POINT('Ctrl Pts',(18.7543554995945,21.328210086877,15.8921156550172));
#190184=CARTESIAN_POINT('Ctrl Pts',(18.7904675704436,21.3275549065075,15.8943844381591));
#190185=CARTESIAN_POINT('Ctrl Pts',(18.8340115187408,21.3256495013035,15.8970659502459));
#190186=CARTESIAN_POINT('Ctrl Pts',(18.8414738174711,21.3252833773237,15.897523565532));
#190187=CARTESIAN_POINT('Ctrl Pts',(18.8530883657383,21.3246518799665,15.8982326484044));
#190188=CARTESIAN_POINT('Ctrl Pts',(18.8572419497409,21.3244137623882,15.8984855997222));
#190189=CARTESIAN_POINT('Ctrl Pts',(18.8649541242802,21.3239488237626,15.8989540628619));
#190190=CARTESIAN_POINT('Ctrl Pts',(18.8685128101065,21.3237252586885,15.899169748845));
#190191=CARTESIAN_POINT('Ctrl Pts',(18.8765703417387,21.3231986242381,15.8996570276594));
#190192=CARTESIAN_POINT('Ctrl Pts',(18.8810687826348,21.3228901734265,15.8999283156869));
#190193=CARTESIAN_POINT('Ctrl Pts',(18.8926787532497,21.3220568210232,15.9006266089437));
#190194=CARTESIAN_POINT('Ctrl Pts',(18.8997887441138,21.3215103515271,15.901052433695));
#190195=CARTESIAN_POINT('Ctrl Pts',(18.9433832031951,21.3179380468659,15.9036529671433));
#190196=CARTESIAN_POINT('Ctrl Pts',(18.9797892582683,21.314001964283,15.9057800767962));
#190197=CARTESIAN_POINT('Ctrl Pts',(19.1851259419455,21.2863959549331,15.9176159526282));
#190198=CARTESIAN_POINT('Ctrl Pts',(19.3508232772645,21.2433198871099,15.9265904750258));
#190199=CARTESIAN_POINT('Ctrl Pts',(19.5983315838293,21.1458696185412,15.9412226533094));
#190200=CARTESIAN_POINT('Ctrl Pts',(19.6846225248531,21.1049649598781,15.9465714627196));
#190201=CARTESIAN_POINT('Ctrl Pts',(19.7865231736233,21.0479380994773,15.9533711087051));
#190202=CARTESIAN_POINT('Ctrl Pts',(19.8050306942982,21.0372091377588,15.9546263239892));
#190203=CARTESIAN_POINT('Ctrl Pts',(19.8310973880839,21.021565519011,15.9564246174336));
#190204=CARTESIAN_POINT('Ctrl Pts',(19.8387930384578,21.01687998381,15.9569593528522));
#190205=CARTESIAN_POINT('Ctrl Pts',(19.852011147903,21.0087159585043,15.9578845469219));
#190206=CARTESIAN_POINT('Ctrl Pts',(19.8575479032991,21.0052607675078,15.9582741443272));
#190207=CARTESIAN_POINT('Ctrl Pts',(19.8681142197278,20.998598812867,15.959021634657));
#190208=CARTESIAN_POINT('Ctrl Pts',(19.8731463853986,20.9953962818427,15.9593793680039));
#190209=CARTESIAN_POINT('Ctrl Pts',(19.8861873008786,20.9870192395026,15.9603110193446));
#190210=CARTESIAN_POINT('Ctrl Pts',(19.8941746799327,20.9818118541448,15.9608861606494));
#190211=CARTESIAN_POINT('Ctrl Pts',(19.9212440039383,20.9639022047959,15.9628509405072));
#190212=CARTESIAN_POINT('Ctrl Pts',(19.9401541806515,20.9509443934031,15.9642501627349));
#190213=CARTESIAN_POINT('Ctrl Pts',(20.1027544055856,20.8356013387163,15.9765200618686));
#190214=CARTESIAN_POINT('Ctrl Pts',(20.2333075397069,20.7159489120623,15.9881030304245));
#190215=CARTESIAN_POINT('Ctrl Pts',(20.4033899281471,20.5157156642508,16.0054603550539));
#190216=CARTESIAN_POINT('Ctrl Pts',(20.4552181534272,20.4465386132608,16.0111498467561));
#190217=CARTESIAN_POINT('Ctrl Pts',(20.5233718654834,20.3429254651327,16.0190667520285));
#190218=CARTESIAN_POINT('Ctrl Pts',(20.5432236627923,20.3109168489621,16.0214351157531));
#190219=CARTESIAN_POINT('Ctrl Pts',(20.5660251228071,20.2718629202117,16.0242178888107));
#190220=CARTESIAN_POINT('Ctrl Pts',(20.5698030123328,20.2653118561174,16.0246811472086));
#190221=CARTESIAN_POINT('Ctrl Pts',(20.5756146198721,20.2551082633819,16.025397051872));
#190222=CARTESIAN_POINT('Ctrl Pts',(20.5776727154793,20.2514697942198,16.0256512273712));
#190223=CARTESIAN_POINT('Ctrl Pts',(20.5814655033656,20.2447180056834,16.0261208109839));
#190224=CARTESIAN_POINT('Ctrl Pts',(20.5832030958854,20.2416064291786,16.0263364004861));
#190225=CARTESIAN_POINT('Ctrl Pts',(20.5871085248795,20.2345711451223,16.0268220143414));
#190226=CARTESIAN_POINT('Ctrl Pts',(20.5892717554082,20.2306449423905,16.0270917427712));
#190227=CARTESIAN_POINT('Ctrl Pts',(20.5956051302825,20.2190631605582,16.0278837328058));
#190228=CARTESIAN_POINT('Ctrl Pts',(20.5997405354619,20.2113885530217,16.0284038314477));
#190229=CARTESIAN_POINT('Ctrl Pts',(20.6288246234771,20.156605750428,16.032084565807));
#190230=CARTESIAN_POINT('Ctrl Pts',(20.6520357953407,20.1085913849861,16.0351439694482));
#190231=CARTESIAN_POINT('Ctrl Pts',(20.6801803883366,20.0442802424138,16.0390920077543));
#190232=CARTESIAN_POINT('Ctrl Pts',(20.6867643316702,20.0287319563941,16.040035283504));
#190233=CARTESIAN_POINT('Ctrl Pts',(20.7494957787683,19.8755090618825,16.049236327001));
#190234=CARTESIAN_POINT('Ctrl Pts',(20.791178896703,19.7323578258933,16.0571182818916));
#190235=CARTESIAN_POINT('Ctrl Pts',(20.8284375704663,19.525355079745,16.0687553370241));
#190236=CARTESIAN_POINT('Ctrl Pts',(20.8367008493418,19.4642511355015,16.0722143614867));
#190237=CARTESIAN_POINT('Ctrl Pts',(20.845656773595,19.3658460812898,16.0778853085104));
#190238=CARTESIAN_POINT('Ctrl Pts',(20.8480505961337,19.3287347319099,16.0800463871473));
#190239=CARTESIAN_POINT('Ctrl Pts',(20.8498893628458,19.2804623105875,16.0828940205839));
#190240=CARTESIAN_POINT('Ctrl Pts',(20.8502252226781,19.2693404503735,16.0835526163589));
#190241=CARTESIAN_POINT('Ctrl Pts',(20.8506288016836,19.2512501195905,16.0846281304933));
#190242=CARTESIAN_POINT('Ctrl Pts',(20.8507498196273,19.2442829621142,16.0850433744891));
#190243=CARTESIAN_POINT('Ctrl Pts',(20.8509163828866,19.2308844498395,16.0858439581539));
#190244=CARTESIAN_POINT('Ctrl Pts',(20.8509670221201,19.2244532271033,16.0862291335997));
#190245=CARTESIAN_POINT('Ctrl Pts',(20.8510158621952,19.2097287994672,16.0871131019139));
#190246=CARTESIAN_POINT('Ctrl Pts',(20.8509946380104,19.2014356748257,16.0876124982341));
#190247=CARTESIAN_POINT('Ctrl Pts',(20.8508088180962,19.1794069845139,16.0889431699681));
#190248=CARTESIAN_POINT('Ctrl Pts',(20.8505592628824,19.1656727041993,16.0897770911394));
#190249=CARTESIAN_POINT('Ctrl Pts',(20.847642924968,19.0611738681957,16.0961556453316));
#190250=CARTESIAN_POINT('Ctrl Pts',(20.8392729666025,18.970674733558,16.1018787170834));
#190251=CARTESIAN_POINT('Ctrl Pts',(20.8032169518968,18.7421961862168,16.1168166293391));
#190252=CARTESIAN_POINT('Ctrl Pts',(20.7675461240913,18.6059206361268,16.1262086367561));
#190253=CARTESIAN_POINT('Ctrl Pts',(20.6997948919733,18.423426085226,16.138950396088));
#190254=CARTESIAN_POINT('Ctrl Pts',(20.6790024772245,18.3733912655459,16.1424578490892));
#190255=CARTESIAN_POINT('Ctrl Pts',(20.6445440617357,18.2986954054887,16.1476623608274));
#190256=CARTESIAN_POINT('Ctrl Pts',(20.6322682925969,18.2734201622335,16.1494176254365));
#190257=CARTESIAN_POINT('Ctrl Pts',(20.6163492017089,18.2422387982106,16.1515689505226));
#190258=CARTESIAN_POINT('Ctrl Pts',(20.6131758667208,18.2360975185967,16.1519919686407));
#190259=CARTESIAN_POINT('Ctrl Pts',(20.6081015072515,18.2263940681131,16.1526591202728));
#190260=CARTESIAN_POINT('Ctrl Pts',(20.6062203077014,18.2228216655634,16.1529044713041));
#190261=CARTESIAN_POINT('Ctrl Pts',(20.6026494985042,18.2160874898472,16.1533664366449));
#190262=CARTESIAN_POINT('Ctrl Pts',(20.6009620989376,18.2129246659584,16.153583179108));
#190263=CARTESIAN_POINT('Ctrl Pts',(20.5970811346228,18.2056945541227,16.1540781451266));
#190264=CARTESIAN_POINT('Ctrl Pts',(20.5948822835497,18.2016301562877,16.1543560288928));
#190265=CARTESIAN_POINT('Ctrl Pts',(20.5889995002765,18.1908408711129,16.1550928209504));
#190266=CARTESIAN_POINT('Ctrl Pts',(20.5852922715274,18.1841286722828,16.1555502857045));
#190267=CARTESIAN_POINT('Ctrl Pts',(20.5587898300362,18.136754170811,16.1587736854552));
#190268=CARTESIAN_POINT('Ctrl Pts',(20.5346916604486,18.0968311278959,16.1614620175247));
#190269=CARTESIAN_POINT('Ctrl Pts',(20.5068104135783,18.0539118424543,16.1643572851687));
#190270=CARTESIAN_POINT('Ctrl Pts',(20.5043155392453,18.0500983423103,16.1646145830395));
#190271=CARTESIAN_POINT('Ctrl Pts',(20.488969728268,18.0268062605546,16.1661865693144));
#190272=CARTESIAN_POINT('Ctrl Pts',(20.4758094394637,18.0075327208593,16.1674893430066));
#190273=CARTESIAN_POINT('Ctrl Pts',(20.4360570578272,17.9513329362194,16.171305918791));
#190274=CARTESIAN_POINT('Ctrl Pts',(20.4085897080285,17.9150413268474,16.1737939066428));
#190275=CARTESIAN_POINT('Ctrl Pts',(20.3112066931709,17.794643740989,16.1822246670852));
#190276=CARTESIAN_POINT('Ctrl Pts',(20.2359567802148,17.7150819033435,16.1881126748508));
#190277=CARTESIAN_POINT('Ctrl Pts',(20.114050299562,17.604703929634,16.1972568195374));
#190278=CARTESIAN_POINT('Ctrl Pts',(20.0717731715553,17.5693276236869,16.2003642261836));
#190279=CARTESIAN_POINT('Ctrl Pts',(20.0010165055719,17.5146701011694,16.2055080717713));
#190280=CARTESIAN_POINT('Ctrl Pts',(19.9733622008392,17.4943616893447,16.2075051263755));
#190281=CARTESIAN_POINT('Ctrl Pts',(19.9363628904862,17.4685507726437,16.2101657079852));
#190282=CARTESIAN_POINT('Ctrl Pts',(19.9274509037726,17.4624346554793,16.2108057081413));
#190283=CARTESIAN_POINT('Ctrl Pts',(19.9127752658781,17.4525275216718,16.2118584073516));
#190284=CARTESIAN_POINT('Ctrl Pts',(19.90703916,17.4486959082331,16.2122695651647));
#190285=CARTESIAN_POINT('Ctrl Pts',(19.895897860404,17.441332219655,16.2130676327694));
#190286=CARTESIAN_POINT('Ctrl Pts',(19.8904950265971,17.437796700086,16.2134544071935));
#190287=CARTESIAN_POINT('Ctrl Pts',(19.8779803864307,17.4296888652459,16.2143497908));
#190288=CARTESIAN_POINT('Ctrl Pts',(19.8708572297909,17.4251343501905,16.2148590561349));
#190289=CARTESIAN_POINT('Ctrl Pts',(19.8516216643843,17.4129969343518,16.2162333858252));
#190290=CARTESIAN_POINT('Ctrl Pts',(19.8394596046722,17.4054939059916,16.2171013783888));
#190291=CARTESIAN_POINT('Ctrl Pts',(19.7271455684354,17.3377652633615,16.225109693091));
#190292=CARTESIAN_POINT('Ctrl Pts',(19.6222596899661,17.2858160057403,16.2325518841576));
#190293=CARTESIAN_POINT('Ctrl Pts',(19.3623086207889,17.1828452886543,16.250815473679));
#190294=CARTESIAN_POINT('Ctrl Pts',(19.2045739553356,17.140554760647,16.261777048255));
#190295=CARTESIAN_POINT('Ctrl Pts',(19.0114487639915,17.1120087278553,16.2741813369229));
#190296=CARTESIAN_POINT('Ctrl Pts',(18.9792379167669,17.108001947539,16.2762152492726));
#190297=CARTESIAN_POINT('Ctrl Pts',(18.9397465779168,17.1040093253315,16.2786560409544));
#190298=CARTESIAN_POINT('Ctrl Pts',(18.932543626788,17.1033183852372,16.2790990806765));
#190299=CARTESIAN_POINT('Ctrl Pts',(18.921245130674,17.1022930161781,16.2797905194299));
#190300=CARTESIAN_POINT('Ctrl Pts',(18.9171519926541,17.1019335641496,16.2800402873708));
#190301=CARTESIAN_POINT('Ctrl Pts',(18.9094985901133,17.1012839043892,16.2805059252253));
#190302=CARTESIAN_POINT('Ctrl Pts',(18.9059386769187,17.1009907936646,16.2807219502892));
#190303=CARTESIAN_POINT('Ctrl Pts',(18.8978098879825,17.1003422066326,16.2812139604061));
#190304=CARTESIAN_POINT('Ctrl Pts',(18.8932405980202,17.0999925549749,16.2814896158611));
#190305=CARTESIAN_POINT('Ctrl Pts',(18.8791897228984,17.0989632329472,16.2823345783945));
#190306=CARTESIAN_POINT('Ctrl Pts',(18.8697045159721,17.0983325739754,16.2829012070692));
#190307=CARTESIAN_POINT('Ctrl Pts',(18.7843094169465,17.0932322598706,16.2879711816293));
#190308=CARTESIAN_POINT('Ctrl Pts',(18.7082055370106,17.0927912042934,16.2922673184702));
#190309=CARTESIAN_POINT('Ctrl Pts',(18.5898142193461,17.0984888947453,16.2988269151612));
#190310=CARTESIAN_POINT('Ctrl Pts',(18.5474631514448,17.1018065770426,16.3011484917261));
#190311=CARTESIAN_POINT('Ctrl Pts',(18.3965607753392,17.1182089445687,16.3094124871073));
#190312=CARTESIAN_POINT('Ctrl Pts',(18.2889612819218,17.1384220680059,16.3152990684544));
#190313=CARTESIAN_POINT('Ctrl Pts',(18.1302306210038,17.181176224433,16.3244398970179));
#190314=CARTESIAN_POINT('Ctrl Pts',(18.0776353898719,17.197568382791,16.3275454029792));
#190315=CARTESIAN_POINT('Ctrl Pts',(17.9934267504993,17.2274637329885,16.3326863827338));
#190316=CARTESIAN_POINT('Ctrl Pts',(17.9613968971506,17.2397189166488,16.3346825297147));
#190317=CARTESIAN_POINT('Ctrl Pts',(17.9196834614535,17.256852010237,16.337342073475));
#190318=CARTESIAN_POINT('Ctrl Pts',(17.9097185867692,17.2610343756639,16.3379819668263));
#190319=CARTESIAN_POINT('Ctrl Pts',(17.8934466771799,17.2680108877178,16.339034535108));
#190320=CARTESIAN_POINT('Ctrl Pts',(17.8871204258572,17.2707599210099,16.3394456695499));
#190321=CARTESIAN_POINT('Ctrl Pts',(17.874898385376,17.2761420960069,16.3402437237786));
#190322=CARTESIAN_POINT('Ctrl Pts',(17.8690009795456,17.2787713939406,16.3406305083675));
#190323=CARTESIAN_POINT('Ctrl Pts',(17.8554086032966,17.2849061140036,16.3415259621137));
#190324=CARTESIAN_POINT('Ctrl Pts',(17.8477224607008,17.288430724232,16.342035287747));
#190325=CARTESIAN_POINT('Ctrl Pts',(17.82710102126,17.2980369714698,16.3434098856754));
#190326=CARTESIAN_POINT('Ctrl Pts',(17.8142060341976,17.3042036419934,16.3442780879574));
#190327=CARTESIAN_POINT('Ctrl Pts',(17.6962262749071,17.3620994183613,16.3523026074465));
#190328=CARTESIAN_POINT('Ctrl Pts',(17.5955586539415,17.422326998344,16.3597622125767));
#190329=CARTESIAN_POINT('Ctrl Pts',(17.367434025814,17.5858981856016,16.3780996977287));
#190330=CARTESIAN_POINT('Ctrl Pts',(17.2459722509986,17.6963277257559,16.389119972739));
#190331=CARTESIAN_POINT('Ctrl Pts',(17.117757460286,17.8433599360849,16.4015037920746));
#190332=CARTESIAN_POINT('Ctrl Pts',(17.0976052266923,17.8675374279079,16.4034746846704));
#190333=CARTESIAN_POINT('Ctrl Pts',(17.0735333306354,17.897763231609,16.4058504009895));
#190334=CARTESIAN_POINT('Ctrl Pts',(17.0690967026126,17.9033924963277,16.4062891936979));
#190335=CARTESIAN_POINT('Ctrl Pts',(17.0621710203954,17.9122723065533,16.4069754851807));
#190336=CARTESIAN_POINT('Ctrl Pts',(17.0596627079737,17.9155076642614,16.4072243201402));
#190337=CARTESIAN_POINT('Ctrl Pts',(17.0549819730716,17.9215814330644,16.4076891564889));
#190338=CARTESIAN_POINT('Ctrl Pts',(17.0528073788356,17.9244180374856,16.4079053073909));
#190339=CARTESIAN_POINT('Ctrl Pts',(17.0478470220042,17.9309225227607,16.4083988249066));
#190340=CARTESIAN_POINT('Ctrl Pts',(17.0450660431875,17.9345939896003,16.4086758541378));
#190341=CARTESIAN_POINT('Ctrl Pts',(17.0378179753301,17.9442281002328,16.4093988628795));
#190342=CARTESIAN_POINT('Ctrl Pts',(17.0333702970708,17.9502053600729,16.4098435184231));
#190343=CARTESIAN_POINT('Ctrl Pts',(17.0039151614196,17.9902297453776,16.4127958637098));
#190344=CARTESIAN_POINT('Ctrl Pts',(16.9798982154478,18.0249978788322,16.4152399451527));
#190345=CARTESIAN_POINT('Ctrl Pts',(16.9164802646476,18.1229502658144,16.4218683499696));
#190346=CARTESIAN_POINT('Ctrl Pts',(16.879345473118,18.1875312487987,16.4259561004834));
#190347=CARTESIAN_POINT('Ctrl Pts',(16.7951473099761,18.3536567690705,16.4361043535853));
#190348=CARTESIAN_POINT('Ctrl Pts',(16.7525863198119,18.4572187109612,16.4421169523245));
#190349=CARTESIAN_POINT('Ctrl Pts',(16.6925866267997,18.6440362425383,16.4530200342531));
#190350=CARTESIAN_POINT('Ctrl Pts',(16.6716050222464,18.7258804430973,16.4578124414119));
#190351=CARTESIAN_POINT('Ctrl Pts',(16.6528673353708,18.8226990582388,16.4636013851176));
#190352=CARTESIAN_POINT('Ctrl Pts',(16.6503087130178,18.8366720756136,16.4644395967754));
#190353=CARTESIAN_POINT('Ctrl Pts',(16.6465902583743,18.8581998192184,16.4657356130468));
#190354=CARTESIAN_POINT('Ctrl Pts',(16.6453303599058,18.8657370144409,16.4661902340614));
#190355=CARTESIAN_POINT('Ctrl Pts',(16.6431068637687,18.879496549896,16.4670218101922));
#190356=CARTESIAN_POINT('Ctrl Pts',(16.6421301613088,18.88571670621,16.4673983444065));
#190357=CARTESIAN_POINT('Ctrl Pts',(16.640058022992,18.8993085841728,16.4682224938568));
#190358=CARTESIAN_POINT('Ctrl Pts',(16.6389737394845,18.9066818978219,16.4686704574311));
#190359=CARTESIAN_POINT('Ctrl Pts',(16.6361094461709,18.9269007237399,16.4699013269525));
#190360=CARTESIAN_POINT('Ctrl Pts',(16.6344085230054,18.9397569491901,16.4706867213659));
#190361=CARTESIAN_POINT('Ctrl Pts',(16.6263685201414,19.0051410896655,16.4746955644089));
#190362=CARTESIAN_POINT('Ctrl Pts',(16.6218825847436,19.057873946071,16.4779768426548));
#190363=CARTESIAN_POINT('Ctrl Pts',(16.6177663611262,19.1446700859844,16.4834601060915));
#190364=CARTESIAN_POINT('Ctrl Pts',(16.616974210654,19.1786565835547,16.4856276638605));
#190365=CARTESIAN_POINT('Ctrl Pts',(16.6171022081697,19.3432687734638,16.496218879237));
#190366=CARTESIAN_POINT('Ctrl Pts',(16.6292932870494,19.473594526131,16.504910420684));
#190367=CARTESIAN_POINT('Ctrl Pts',(16.6709615317538,19.6953469514709,16.5197603295542));
#190368=CARTESIAN_POINT('Ctrl Pts',(16.6947819252022,19.7874664799454,16.5259401167032));
#190369=CARTESIAN_POINT('Ctrl Pts',(16.7277657538097,19.8868749541636,16.5324111822769));
#190370=CARTESIAN_POINT('Ctrl Pts',(16.7308789356001,19.8960465778259,16.5330062690486));
#190371=CARTESIAN_POINT('Ctrl Pts',(16.7355692054707,19.9095590038365,16.5338797830683));
#190372=CARTESIAN_POINT('Ctrl Pts',(16.7370976771217,19.9139163792231,16.5341609699816));
#190373=CARTESIAN_POINT('Ctrl Pts',(16.7398349366887,19.9216387860205,16.5346583799414));
#190374=CARTESIAN_POINT('Ctrl Pts',(16.7410380033822,19.9250057875421,16.5348749372459));
#190375=CARTESIAN_POINT('Ctrl Pts',(16.7432997957639,19.931285569357,16.5352782394492));
#190376=CARTESIAN_POINT('Ctrl Pts',(16.7443563783493,19.9341990484388,16.5354651119654));
#190377=CARTESIAN_POINT('Ctrl Pts',(16.7454193623258,19.9371102171621,16.5356516081066));
#190378=CARTESIAN_POINT('Origin',(18.734,19.211,0.));
#190379=CARTESIAN_POINT('',(16.7454193509487,19.937110186004,17.5536949115506));
#190380=CARTESIAN_POINT('',(16.7454194652257,19.9371104989717,17.3329785907215));
#190381=CARTESIAN_POINT('',(16.7454193623258,19.9371102171621,0.));
#190382=CARTESIAN_POINT('',(16.6170009797991,19.2127872412316,17.5117108633035));
#190383=CARTESIAN_POINT('Ctrl Pts',(16.7454193509487,19.937110186004,17.5536949115506));
#190384=CARTESIAN_POINT('Ctrl Pts',(16.7414203484773,19.9261582133096,17.5529593386965));
#190385=CARTESIAN_POINT('Ctrl Pts',(16.7375110411194,19.9151710662913,17.5522275673665));
#190386=CARTESIAN_POINT('Ctrl Pts',(16.7285976735804,19.8894486603001,17.5505296495991));
#190387=CARTESIAN_POINT('Ctrl Pts',(16.7236654571562,19.874691294042,17.5495671222079));
#190388=CARTESIAN_POINT('Ctrl Pts',(16.71712756313,19.8543878070169,17.5482599832547));
#190389=CARTESIAN_POINT('Ctrl Pts',(16.7153813400418,19.8488879245489,17.5479076128735));
#190390=CARTESIAN_POINT('Ctrl Pts',(16.7126398285665,19.8401292920733,17.5473492557316));
#190391=CARTESIAN_POINT('Ctrl Pts',(16.7116298969789,19.8368752076809,17.5471424223113));
#190392=CARTESIAN_POINT('Ctrl Pts',(16.7095583186972,19.8301430390956,17.5467158036132));
#190393=CARTESIAN_POINT('Ctrl Pts',(16.7084977766896,19.8266646549669,17.5464960889765));
#190394=CARTESIAN_POINT('Ctrl Pts',(16.7059888775804,19.8183592714762,17.5459731353955));
#190395=CARTESIAN_POINT('Ctrl Pts',(16.7045487725742,19.8135297619212,17.545670377959));
#190396=CARTESIAN_POINT('Ctrl Pts',(16.6997356750759,19.7971756124328,17.5446495209159));
#190397=CARTESIAN_POINT('Ctrl Pts',(16.6964434236498,19.785627188258,17.5439359715136));
#190398=CARTESIAN_POINT('Ctrl Pts',(16.6887613677531,19.7577839608348,17.5422317975928));
#190399=CARTESIAN_POINT('Ctrl Pts',(16.6844677230005,19.7414632360976,17.5412461317108));
#190400=CARTESIAN_POINT('Ctrl Pts',(16.6690505818285,19.6798768158442,17.5375704593111));
#190401=CARTESIAN_POINT('Ctrl Pts',(16.6592272448662,19.6342967519587,17.5349384179573));
#190402=CARTESIAN_POINT('Ctrl Pts',(16.6284575288223,19.4644733677277,17.5253353954585));
#190403=CARTESIAN_POINT('Ctrl Pts',(16.6171072209053,19.3387629515357,17.518611897998));
#190404=CARTESIAN_POINT('Ctrl Pts',(16.6170007560366,19.2127891501584,17.5117113586358));
#190405=CARTESIAN_POINT('Ctrl Pts',(16.6170007544063,19.2127872200763,17.5117112529106));
#190406=CARTESIAN_POINT('Ctrl Pts',(16.616930473988,19.1295386070637,17.5071510947737));
#190407=CARTESIAN_POINT('Ctrl Pts',(16.6217706304624,19.0463629764936,17.5025270244436));
#190408=CARTESIAN_POINT('Ctrl Pts',(16.6354866257038,18.9297561389935,17.4958024094825));
#190409=CARTESIAN_POINT('Ctrl Pts',(16.6402990166117,18.8959246220188,17.4938228583187));
#190410=CARTESIAN_POINT('Ctrl Pts',(16.6476156658052,18.8521206747072,17.4912164872332));
#190411=CARTESIAN_POINT('Ctrl Pts',(16.649376831497,18.8420281854468,17.4906129779659));
#190412=CARTESIAN_POINT('Ctrl Pts',(16.6524780221122,18.8249879314239,17.4895887618969));
#190413=CARTESIAN_POINT('Ctrl Pts',(16.6537797605833,18.8180333154182,17.4891692683912));
#190414=CARTESIAN_POINT('Ctrl Pts',(16.6564245117204,18.8042850546055,17.4883369974055));
#190415=CARTESIAN_POINT('Ctrl Pts',(16.6577660445911,18.7974912129556,17.4879242716445));
#190416=CARTESIAN_POINT('Ctrl Pts',(16.6604207091026,18.784386028315,17.4871252790189));
#190417=CARTESIAN_POINT('Ctrl Pts',(16.6617293838868,18.7780738531304,17.4867391587643));
#190418=CARTESIAN_POINT('Ctrl Pts',(16.6648076564294,18.7635601250018,17.4858483485752));
#190419=CARTESIAN_POINT('Ctrl Pts',(16.6665972140381,18.755362958199,17.4853430235871));
#190420=CARTESIAN_POINT('Ctrl Pts',(16.6715176924695,18.733450374863,17.4839861829964));
#190421=CARTESIAN_POINT('Ctrl Pts',(16.6747366394142,18.7197553459859,17.4831318540082));
#190422=CARTESIAN_POINT('Ctrl Pts',(16.7030000973699,18.6046704834507,17.475898054269));
#190423=CARTESIAN_POINT('Ctrl Pts',(16.7353754886842,18.5052447401283,17.4692799484978));
#190424=CARTESIAN_POINT('Ctrl Pts',(16.8068616716935,18.330706537951,17.4570211598824));
#190425=CARTESIAN_POINT('Ctrl Pts',(16.84339386114,18.2547646976231,17.4514527207453));
#190426=CARTESIAN_POINT('Ctrl Pts',(16.9294015456653,18.1002834487083,17.4397718882579));
#190427=CARTESIAN_POINT('Ctrl Pts',(16.9797192639681,18.0224006313024,17.4336727871492));
#190428=CARTESIAN_POINT('Ctrl Pts',(17.0536149814904,17.922989537048,17.4258114738714));
#190429=CARTESIAN_POINT('Ctrl Pts',(17.0728039593309,17.8983337371465,17.4238554125912));
#190430=CARTESIAN_POINT('Ctrl Pts',(17.0970484780719,17.8685657004768,17.421495043113));
#190431=CARTESIAN_POINT('Ctrl Pts',(17.1015923491996,17.8630439923162,17.4210572723664));
#190432=CARTESIAN_POINT('Ctrl Pts',(17.1087791026728,17.8544002934178,17.4203722198341));
#190433=CARTESIAN_POINT('Ctrl Pts',(17.1114031545307,17.8512628170358,17.4201236096888));
#190434=CARTESIAN_POINT('Ctrl Pts',(17.1163377107054,17.8453973866933,17.4196589644846));
#190435=CARTESIAN_POINT('Ctrl Pts',(17.1186460052478,17.842667711582,17.4194427812764));
#190436=CARTESIAN_POINT('Ctrl Pts',(17.1239478200855,17.8364301605862,17.4189488915101));
#190437=CARTESIAN_POINT('Ctrl Pts',(17.1269458898656,17.8329262162364,17.418671524249));
#190438=CARTESIAN_POINT('Ctrl Pts',(17.1348298900091,17.8237726398275,17.4179470525435));
#190439=CARTESIAN_POINT('Ctrl Pts',(17.1397343612873,17.8181389636981,17.4175012808001));
#190440=CARTESIAN_POINT('Ctrl Pts',(17.1728156020896,17.7805428039361,17.4145262679844));
#190441=CARTESIAN_POINT('Ctrl Pts',(17.2019240875876,17.749408927122,17.4120617505356));
#190442=CARTESIAN_POINT('Ctrl Pts',(17.2835612398275,17.6672126147658,17.4054834610824));
#190443=CARTESIAN_POINT('Ctrl Pts',(17.3378328228301,17.6179617963119,17.4014605943982));
#190444=CARTESIAN_POINT('Ctrl Pts',(17.4635842510242,17.5152170791767,17.3926105447383));
#190445=CARTESIAN_POINT('Ctrl Pts',(17.5361100384896,17.4632313231011,17.3878053013982));
#190446=CARTESIAN_POINT('Ctrl Pts',(17.6722748825049,17.3780970939397,17.3789766371124));
#190447=CARTESIAN_POINT('Ctrl Pts',(17.7347273956491,17.3433152454516,17.3749940799317));
#190448=CARTESIAN_POINT('Ctrl Pts',(17.8232465646735,17.2997284884751,17.3693501776409));
#190449=CARTESIAN_POINT('Ctrl Pts',(17.8479069289927,17.2881714621802,17.3677782221454));
#190450=CARTESIAN_POINT('Ctrl Pts',(17.8909907883034,17.2689851299114,17.3650281590181));
#190451=CARTESIAN_POINT('Ctrl Pts',(17.9093120960237,17.2611343360064,17.363857573677));
#190452=CARTESIAN_POINT('Ctrl Pts',(17.9358134126304,17.2502186788277,17.3621616175449));
#190453=CARTESIAN_POINT('Ctrl Pts',(17.9439061442885,17.2469437601221,17.3616433615108));
#190454=CARTESIAN_POINT('Ctrl Pts',(17.9580666703696,17.2413150445504,17.3607358023873));
#190455=CARTESIAN_POINT('Ctrl Pts',(17.9641255312305,17.2389389825277,17.3603472556564));
#190456=CARTESIAN_POINT('Ctrl Pts',(17.97577869884,17.2344309272184,17.3595994741014));
#190457=CARTESIAN_POINT('Ctrl Pts',(17.9813712894228,17.2322946495549,17.3592403877503));
#190458=CARTESIAN_POINT('Ctrl Pts',(17.9960068062144,17.2267751472188,17.3583000898127));
#190459=CARTESIAN_POINT('Ctrl Pts',(18.0050638725999,17.2234300420342,17.3577176096683));
#190460=CARTESIAN_POINT('Ctrl Pts',(18.0363822393942,17.2121058840081,17.3557012625556));
#190461=CARTESIAN_POINT('Ctrl Pts',(18.0587535187793,17.2044381780524,17.3542571197202));
#190462=CARTESIAN_POINT('Ctrl Pts',(18.2381690003453,17.146284060849,17.3426406855067));
#190463=CARTESIAN_POINT('Ctrl Pts',(18.4004692061848,17.1139454284606,17.3318560948795));
#190464=CARTESIAN_POINT('Ctrl Pts',(18.6921302354154,17.0905654657266,17.3125201350039));
#190465=CARTESIAN_POINT('Ctrl Pts',(18.8200952954898,17.0918987612435,17.3040735677056));
#190466=CARTESIAN_POINT('Ctrl Pts',(18.9590371432447,17.1059609150673,17.2954131970075));
#190467=CARTESIAN_POINT('Ctrl Pts',(18.9708939612514,17.1072622475489,17.294678389854));
#190468=CARTESIAN_POINT('Ctrl Pts',(18.9877305204638,17.1092542774094,17.2936416071261));
#190469=CARTESIAN_POINT('Ctrl Pts',(18.9927195257287,17.1098625776392,17.2933352176531));
#190470=CARTESIAN_POINT('Ctrl Pts',(19.0013121031797,17.1109413232773,17.2928090081105));
#190471=CARTESIAN_POINT('Ctrl Pts',(19.0049167015928,17.1114032892573,17.2925887141459));
#190472=CARTESIAN_POINT('Ctrl Pts',(19.0119022544193,17.112316848304,17.2921626898538));
#190473=CARTESIAN_POINT('Ctrl Pts',(19.0152833066568,17.1127673303466,17.2919568956588));
#190474=CARTESIAN_POINT('Ctrl Pts',(19.0244000666724,17.1140044544689,17.2914030419323));
#190475=CARTESIAN_POINT('Ctrl Pts',(19.0301337095775,17.1148064630038,17.2910558438993));
#190476=CARTESIAN_POINT('Ctrl Pts',(19.0513878827432,17.1178683934739,17.2897727522869));
#190477=CARTESIAN_POINT('Ctrl Pts',(19.0668868804549,17.1202773144989,17.2888449040199));
#190478=CARTESIAN_POINT('Ctrl Pts',(19.2153882629564,17.1450513384769,17.280017649029));
#190479=CARTESIAN_POINT('Ctrl Pts',(19.346012391733,17.1799093107208,17.2727250319537));
#190480=CARTESIAN_POINT('Ctrl Pts',(19.618846629008,17.281456511595,17.2569159311043));
#190481=CARTESIAN_POINT('Ctrl Pts',(19.7587481388918,17.3519746174461,17.2484122719691));
#190482=CARTESIAN_POINT('Ctrl Pts',(19.9074393412255,17.4488474200087,17.2380773236331));
#190483=CARTESIAN_POINT('Ctrl Pts',(19.9250879514431,17.460728293646,17.236828896074));
#190484=CARTESIAN_POINT('Ctrl Pts',(19.9499351351986,17.478005029731,17.2350386566563));
#190485=CARTESIAN_POINT('Ctrl Pts',(19.9572833632808,17.4831841448488,17.2345050845135));
#190486=CARTESIAN_POINT('Ctrl Pts',(19.9699058781282,17.492201522096,17.2335812678179));
#190487=CARTESIAN_POINT('Ctrl Pts',(19.9751958619946,17.4960176741622,17.2331918776204));
#190488=CARTESIAN_POINT('Ctrl Pts',(19.9852927117957,17.5033726466368,17.2324443409335));
#190489=CARTESIAN_POINT('Ctrl Pts',(19.9901024196535,17.506907473535,17.2320863518811));
#190490=CARTESIAN_POINT('Ctrl Pts',(20.0025746258844,17.5161552372449,17.2311530586132));
#190491=CARTESIAN_POINT('Ctrl Pts',(20.0102134354006,17.5218997620351,17.2305765225276));
#190492=CARTESIAN_POINT('Ctrl Pts',(20.0361503299252,17.541681166325,17.2286018776703));
#190493=CARTESIAN_POINT('Ctrl Pts',(20.0542573221229,17.5559648379697,17.2271940542857));
#190494=CARTESIAN_POINT('Ctrl Pts',(20.2073793976364,17.6808669288303,17.2150304062749));
#190495=CARTESIAN_POINT('Ctrl Pts',(20.328444417153,17.8074765799318,17.2035794475477));
#190496=CARTESIAN_POINT('Ctrl Pts',(20.4849106737322,18.0178159966541,17.1862579529661));
#190497=CARTESIAN_POINT('Ctrl Pts',(20.5328232904217,18.0913514136052,17.1804778773838));
#190498=CARTESIAN_POINT('Ctrl Pts',(20.5947632614437,18.2007067832672,17.1724526911396));
#190499=CARTESIAN_POINT('Ctrl Pts',(20.6125949374181,18.234263712583,17.1700627034925));
#190500=CARTESIAN_POINT('Ctrl Pts',(20.6328909410748,18.2750728286973,17.1672580005521));
#190501=CARTESIAN_POINT('Ctrl Pts',(20.6362305181192,18.2818791596311,17.166793555187));
#190502=CARTESIAN_POINT('Ctrl Pts',(20.6413564681519,18.2924697544619,17.1660762162998));
#190503=CARTESIAN_POINT('Ctrl Pts',(20.6431682672592,18.2962415419581,17.1658217838991));
#190504=CARTESIAN_POINT('Ctrl Pts',(20.646502347866,18.3032354554579,17.1653519628884));
#190505=CARTESIAN_POINT('Ctrl Pts',(20.6480276637371,18.3064560255739,17.165136391378));
#190506=CARTESIAN_POINT('Ctrl Pts',(20.6514510839316,18.313731708694,17.1646511167101));
#190507=CARTESIAN_POINT('Ctrl Pts',(20.6533444549331,18.3177889890859,17.1643817076547));
#190508=CARTESIAN_POINT('Ctrl Pts',(20.6588758918186,18.3297410353772,17.1635915240095));
#190509=CARTESIAN_POINT('Ctrl Pts',(20.6624782718708,18.3376523473332,17.163072897647));
#190510=CARTESIAN_POINT('Ctrl Pts',(20.6876027188414,18.3937425194552,17.1594254734656));
#190511=CARTESIAN_POINT('Ctrl Pts',(20.7073674778092,18.4426933163723,17.156395851925));
#190512=CARTESIAN_POINT('Ctrl Pts',(20.7307136085991,18.5073810616213,17.1525263830605));
#190513=CARTESIAN_POINT('Ctrl Pts',(20.7359729435373,18.5224876930344,17.151632075838));
#190514=CARTESIAN_POINT('Ctrl Pts',(20.7571582551636,18.5856352070148,17.1479270871854));
#190515=CARTESIAN_POINT('Ctrl Pts',(20.7715305716548,18.6341811708897,17.1451583091965));
#190516=CARTESIAN_POINT('Ctrl Pts',(20.8114262041999,18.7891481114983,17.136445862166));
#190517=CARTESIAN_POINT('Ctrl Pts',(20.8304482396653,18.8970532673305,17.1305550253318));
#190518=CARTESIAN_POINT('Ctrl Pts',(20.8463899414147,19.0608590013463,17.1214043031633));
#190519=CARTESIAN_POINT('Ctrl Pts',(20.8495851896341,19.1159618914489,17.118293126052));
#190520=CARTESIAN_POINT('Ctrl Pts',(20.8512712110308,19.2054561438526,17.1131435958702));
#190521=CARTESIAN_POINT('Ctrl Pts',(20.8510825746819,19.2397974004838,17.1111447413852));
#190522=CARTESIAN_POINT('Ctrl Pts',(20.8497365106307,19.2849251393151,17.1084821016704));
#190523=CARTESIAN_POINT('Ctrl Pts',(20.849331352959,19.2957299785332,17.1078418897695));
#190524=CARTESIAN_POINT('Ctrl Pts',(20.8485321285317,19.3134230094889,17.106788930932));
#190525=CARTESIAN_POINT('Ctrl Pts',(20.8481871241254,19.3203133016414,17.1063777267286));
#190526=CARTESIAN_POINT('Ctrl Pts',(20.8474540518868,19.3336485109807,17.105579632429));
#190527=CARTESIAN_POINT('Ctrl Pts',(20.8470701669998,19.3400935884754,17.1051928780356));
#190528=CARTESIAN_POINT('Ctrl Pts',(20.8461156322335,19.3549722417584,17.1042976330661));
#190529=CARTESIAN_POINT('Ctrl Pts',(20.8455239453633,19.3634043150389,17.1037884869775));
#190530=CARTESIAN_POINT('Ctrl Pts',(20.8437966433915,19.3860746690637,17.1024146878706));
#190531=CARTESIAN_POINT('Ctrl Pts',(20.8425674160037,19.4003051839901,17.1015471101614));
#190532=CARTESIAN_POINT('Ctrl Pts',(20.8276357658058,19.5549022464232,17.0920635745424));
#190533=CARTESIAN_POINT('Ctrl Pts',(20.800086049783,19.6935500670748,17.0829980847195));
#190534=CARTESIAN_POINT('Ctrl Pts',(20.7307977874838,19.9208012566434,17.0673681974679));
#190535=CARTESIAN_POINT('Ctrl Pts',(20.6963367493345,20.011158676072,17.0609429129385));
#190536=CARTESIAN_POINT('Ctrl Pts',(20.6352759178837,20.1433303756454,17.0514418293443));
#190537=CARTESIAN_POINT('Ctrl Pts',(20.6131859944018,20.1870894826534,17.0482795978475));
#190538=CARTESIAN_POINT('Ctrl Pts',(20.5769535408538,20.2530657487165,17.0435263954882));
#190539=CARTESIAN_POINT('Ctrl Pts',(20.5638832171873,20.2758503823164,17.0418877376068));
#190540=CARTESIAN_POINT('Ctrl Pts',(20.5469192652692,20.3041872837718,17.039858978104));
#190541=CARTESIAN_POINT('Ctrl Pts',(20.5434191230558,20.3099709458204,17.0394453929742));
#190542=CARTESIAN_POINT('Ctrl Pts',(20.5378020768602,20.3191530109787,17.0387897005556));
#190543=CARTESIAN_POINT('Ctrl Pts',(20.535703167923,20.3225622895445,17.038546444553));
#190544=CARTESIAN_POINT('Ctrl Pts',(20.5317022680612,20.3290198856707,17.0380861006124));
#190545=CARTESIAN_POINT('Ctrl Pts',(20.5298022124471,20.3320692767492,17.0378688976334));
#190546=CARTESIAN_POINT('Ctrl Pts',(20.525408522584,20.3390808577069,17.0373698646123));
#190547=CARTESIAN_POINT('Ctrl Pts',(20.5229095033285,20.3430396221755,17.037088394243));
#190548=CARTESIAN_POINT('Ctrl Pts',(20.5161719682598,20.3536347098248,17.036335753413));
#190549=CARTESIAN_POINT('Ctrl Pts',(20.5119094776156,20.3602558019482,17.0358661267749));
#190550=CARTESIAN_POINT('Ctrl Pts',(20.4795886579271,20.4098508002853,17.0323525780418));
#190551=CARTESIAN_POINT('Ctrl Pts',(20.4500104122655,20.4518191597275,17.0294028668135));
#190552=CARTESIAN_POINT('Ctrl Pts',(20.4053607853312,20.5105171054204,17.0252482225053));
#190553=CARTESIAN_POINT('Ctrl Pts',(20.3915053631782,20.528143728822,17.0239966578021));
#190554=CARTESIAN_POINT('Ctrl Pts',(20.3484468106026,20.5811663733807,17.0202087884638));
#190555=CARTESIAN_POINT('Ctrl Pts',(20.3183701347066,20.6158366138006,17.0176997317918));
#190556=CARTESIAN_POINT('Ctrl Pts',(20.2128849770733,20.7297317374043,17.0092478498465));
#190557=CARTESIAN_POINT('Ctrl Pts',(20.1324763160936,20.8040819111105,17.003359649536));
#190558=CARTESIAN_POINT('Ctrl Pts',(20.0034491766804,20.9060590566062,16.9942150573862));
#190559=CARTESIAN_POINT('Ctrl Pts',(19.9588952919317,20.9385292460355,16.9911073943248));
#190560=CARTESIAN_POINT('Ctrl Pts',(19.8846331954191,20.9883320871173,16.9859631620631));
#190561=CARTESIAN_POINT('Ctrl Pts',(19.8556797664559,21.0067450830241,16.9839659849589));
#190562=CARTESIAN_POINT('Ctrl Pts',(19.8170337082652,21.0300227657868,16.9813052632023));
#190563=CARTESIAN_POINT('Ctrl Pts',(19.8077321066733,21.0355287589483,16.980665248559));
#190564=CARTESIAN_POINT('Ctrl Pts',(19.7924259741928,21.0444314937842,16.9796125315376));
#190565=CARTESIAN_POINT('Ctrl Pts',(19.7864462110751,21.0478705877955,16.9792013705023));
#190566=CARTESIAN_POINT('Ctrl Pts',(19.7748369701807,21.0544720209546,16.9784033009444));
#190567=CARTESIAN_POINT('Ctrl Pts',(19.7692096168251,21.0576379554037,16.9780165278119));
#190568=CARTESIAN_POINT('Ctrl Pts',(19.7561804678972,21.064889848985,16.9771211534612));
#190569=CARTESIAN_POINT('Ctrl Pts',(19.7487685396473,21.0689572892891,16.9766118961335));
#190570=CARTESIAN_POINT('Ctrl Pts',(19.7287641987546,21.0797796511759,16.9752376022316));
#190571=CARTESIAN_POINT('Ctrl Pts',(19.7161275964603,21.0864515627783,16.9743696376872));
#190572=CARTESIAN_POINT('Ctrl Pts',(19.5995630777364,21.1464945087051,16.9663634624318));
#190573=CARTESIAN_POINT('Ctrl Pts',(19.4914683028102,21.1912960388545,16.9589235698457));
#190574=CARTESIAN_POINT('Ctrl Pts',(19.2253450817259,21.2766062084589,16.9406693399547));
#190575=CARTESIAN_POINT('Ctrl Pts',(19.0652416449195,21.3082429602711,16.9297150924791));
#190576=CARTESIAN_POINT('Ctrl Pts',(18.8706224461329,21.3238380446791,16.9173081087366));
#190577=CARTESIAN_POINT('Ctrl Pts',(18.8380911363972,21.3256904268354,16.9152661940177));
#190578=CARTESIAN_POINT('Ctrl Pts',(18.7982878150827,21.327036048333,16.9128171542623));
#190579=CARTESIAN_POINT('Ctrl Pts',(18.79104624345,21.3272436557768,16.9123735860038));
#190580=CARTESIAN_POINT('Ctrl Pts',(18.7796940488719,21.3275107965473,16.9116815068343));
#190581=CARTESIAN_POINT('Ctrl Pts',(18.7755841549982,21.3275955345131,16.9114316229184));
#190582=CARTESIAN_POINT('Ctrl Pts',(18.7679028238339,21.3277315266311,16.9109658844978));
#190583=CARTESIAN_POINT('Ctrl Pts',(18.7643315428923,21.3277857130647,16.9107498741445));
#190584=CARTESIAN_POINT('Ctrl Pts',(18.7561806632489,21.3278887529587,16.9102580471941));
#190585=CARTESIAN_POINT('Ctrl Pts',(18.7516010414213,21.3279317840853,16.9099825592453));
#190586=CARTESIAN_POINT('Ctrl Pts',(18.737529994505,21.3280183340717,16.9091386203851));
#190587=CARTESIAN_POINT('Ctrl Pts',(18.728038236965,21.3280128843792,16.9085728384662));
#190588=CARTESIAN_POINT('Ctrl Pts',(18.6430857502993,21.3273927443314,16.9035378425769));
#190589=CARTESIAN_POINT('Ctrl Pts',(18.5676994108747,21.3228073609024,16.8992726834526));
#190590=CARTESIAN_POINT('Ctrl Pts',(18.4499369703859,21.3092971492502,16.8927104657092));
#190591=CARTESIAN_POINT('Ctrl Pts',(18.4073210773131,21.3030859934696,16.8903567839326));
#190592=CARTESIAN_POINT('Ctrl Pts',(18.257273188316,21.2765198749099,16.88206062279));
#190593=CARTESIAN_POINT('Ctrl Pts',(18.1512622912255,21.2491503091685,16.8761737784865));
#190594=CARTESIAN_POINT('Ctrl Pts',(17.9957374727907,21.1958655312112,16.8670323388026));
#190595=CARTESIAN_POINT('Ctrl Pts',(17.944351198209,21.1759877509655,16.8639264826521));
#190596=CARTESIAN_POINT('Ctrl Pts',(17.8623236988634,21.1405194965256,16.8587849748045));
#190597=CARTESIAN_POINT('Ctrl Pts',(17.8311832956771,21.1261466950256,16.8567886605093));
#190598=CARTESIAN_POINT('Ctrl Pts',(17.7907072919277,21.1062584691937,16.8541289253531));
#190599=CARTESIAN_POINT('Ctrl Pts',(17.7810444136654,21.1014183246231,16.8534890122342));
#190600=CARTESIAN_POINT('Ctrl Pts',(17.7652756103087,21.0933680928034,16.8524364196687));
#190601=CARTESIAN_POINT('Ctrl Pts',(17.75914749017,21.0902017354009,16.8520252808494));
#190602=CARTESIAN_POINT('Ctrl Pts',(17.7473130818168,21.084013512501,16.8512272240081));
#190603=CARTESIAN_POINT('Ctrl Pts',(17.7416049228073,21.0809953748221,16.8508404412153));
#190604=CARTESIAN_POINT('Ctrl Pts',(17.7284538494114,21.0739646899568,16.8499450002009));
#190605=CARTESIAN_POINT('Ctrl Pts',(17.7210210265246,21.0699335902732,16.8494356855626));
#190606=CARTESIAN_POINT('Ctrl Pts',(17.7010895427968,21.0589689596216,16.8480611367164));
#190607=CARTESIAN_POINT('Ctrl Pts',(17.6886367880156,21.0519532931682,16.8471929728479));
#190608=CARTESIAN_POINT('Ctrl Pts',(17.5748395001307,20.9863149641814,16.8391714645458));
#190609=CARTESIAN_POINT('Ctrl Pts',(17.4784668057012,20.9195153888113,16.8317150962354));
#190610=CARTESIAN_POINT('Ctrl Pts',(17.2619534841887,20.7411909050002,16.8133917575097));
#190611=CARTESIAN_POINT('Ctrl Pts',(17.1482481552742,20.6230185634499,16.8023828327524));
#190612=CARTESIAN_POINT('Ctrl Pts',(17.0301009742324,20.4677494869167,16.7899952032352));
#190613=CARTESIAN_POINT('Ctrl Pts',(17.011497487052,20.4421281432195,16.7880122696032));
#190614=CARTESIAN_POINT('Ctrl Pts',(16.9893870660052,20.4101940089906,16.7856241026111));
#190615=CARTESIAN_POINT('Ctrl Pts',(16.9853295342578,20.4042695279387,16.7851844865034));
#190616=CARTESIAN_POINT('Ctrl Pts',(16.9790045276265,20.3949327154509,16.7844971968478));
#190617=CARTESIAN_POINT('Ctrl Pts',(16.9767167238365,20.3915343157823,16.7842481807965));
#190618=CARTESIAN_POINT('Ctrl Pts',(16.9724515995538,20.3851588500349,16.7837831898338));
#190619=CARTESIAN_POINT('Ctrl Pts',(16.9704719751159,20.3821834518541,16.783567064313));
#190620=CARTESIAN_POINT('Ctrl Pts',(16.9659608172581,20.3753657583851,16.7830738437987));
#190621=CARTESIAN_POINT('Ctrl Pts',(16.9634342741474,20.3715202205749,16.7827970846572));
#190622=CARTESIAN_POINT('Ctrl Pts',(16.956857907152,20.3614391611396,16.7820752443567));
#190623=CARTESIAN_POINT('Ctrl Pts',(16.952828319885,20.3551904261489,16.7816314802075));
#190624=CARTESIAN_POINT('Ctrl Pts',(16.9262800447879,20.3135415232443,16.7786970898218));
#190625=CARTESIAN_POINT('Ctrl Pts',(16.9047834059043,20.2774972702517,16.7762691956215));
#190626=CARTESIAN_POINT('Ctrl Pts',(16.8738106304476,20.2218688113429,16.7726515058379));
#190627=CARTESIAN_POINT('Ctrl Pts',(16.8635425440734,20.202740490925,16.7714299744964));
#190628=CARTESIAN_POINT('Ctrl Pts',(16.8457274024794,20.1682915448323,16.7692639724233));
#190629=CARTESIAN_POINT('Ctrl Pts',(16.8380682053848,20.1530313973742,16.7683161241542));
#190630=CARTESIAN_POINT('Ctrl Pts',(16.7987610646652,20.072294322494,16.7633540324268));
#190631=CARTESIAN_POINT('Ctrl Pts',(16.7703355363631,20.0053475663791,16.7594186474677));
#190632=CARTESIAN_POINT('Ctrl Pts',(16.745419290545,19.9371100205779,16.7554728823802));
#190633=CARTESIAN_POINT('',(16.6170000778107,19.2115739777624,17.2909082101745));
#190634=CARTESIAN_POINT('Ctrl Pts',(16.7454193623258,19.9371102171621,16.5356516081066));
#190635=CARTESIAN_POINT('Ctrl Pts',(16.7457579270419,19.9380374362303,16.5357110078854));
#190636=CARTESIAN_POINT('Ctrl Pts',(16.746097141146,19.9389644209246,16.535770369483));
#190637=CARTESIAN_POINT('Ctrl Pts',(16.7488929535339,19.9465881286455,16.5362583831511));
#190638=CARTESIAN_POINT('Ctrl Pts',(16.7513827741961,19.9532727397506,16.5366850890955));
#190639=CARTESIAN_POINT('Ctrl Pts',(16.7648702367006,19.9889314964981,16.5389555861235));
#190640=CARTESIAN_POINT('Ctrl Pts',(16.7764699454952,20.0176757416178,16.5407654918082));
#190641=CARTESIAN_POINT('Ctrl Pts',(16.8532263803271,20.1964619756451,16.5519560748687));
#190642=CARTESIAN_POINT('Ctrl Pts',(16.9349647288499,20.3387983677051,16.5606012098924));
#190643=CARTESIAN_POINT('Ctrl Pts',(17.1022875670835,20.5649019296998,16.5759957205492));
#190644=CARTESIAN_POINT('Ctrl Pts',(17.1800410112516,20.653477735829,16.5825621375124));
#190645=CARTESIAN_POINT('Ctrl Pts',(17.2750386749147,20.745055200382,16.5902921444315));
#190646=CARTESIAN_POINT('Ctrl Pts',(17.2854344415822,20.7548754204719,16.5911342712664));
#190647=CARTESIAN_POINT('Ctrl Pts',(17.302135585813,20.7703347407435,16.592481656417));
#190648=CARTESIAN_POINT('Ctrl Pts',(17.308376759431,20.7760427812323,16.5929839679614));
#190649=CARTESIAN_POINT('Ctrl Pts',(17.319442938089,20.78604254412,16.5938725911452));
#190650=CARTESIAN_POINT('Ctrl Pts',(17.3242537156305,20.7903499008994,16.5942582357428));
#190651=CARTESIAN_POINT('Ctrl Pts',(17.3342433739037,20.7992121883772,16.5950577050286));
#190652=CARTESIAN_POINT('Ctrl Pts',(17.3394249520335,20.803763950323,16.5954716555505));
#190653=CARTESIAN_POINT('Ctrl Pts',(17.3527797461909,20.8153803540355,16.5965367467642));
#190654=CARTESIAN_POINT('Ctrl Pts',(17.3609848906973,20.8224078356514,16.5971894146369));
#190655=CARTESIAN_POINT('Ctrl Pts',(17.3954326590546,20.8514572865475,16.5999226849536));
#190656=CARTESIAN_POINT('Ctrl Pts',(17.4221529064202,20.8729024107565,16.6020265592615));
#190657=CARTESIAN_POINT('Ctrl Pts',(17.4930983449378,20.9270644688671,16.6075743411489));
#190658=CARTESIAN_POINT('Ctrl Pts',(17.5380969765532,20.9587211793533,16.6110565188951));
#190659=CARTESIAN_POINT('Ctrl Pts',(17.6611866071554,21.0383342983285,16.62047828248));
#190660=CARTESIAN_POINT('Ctrl Pts',(17.7412413697173,21.0830329263447,16.6265050377394));
#190661=CARTESIAN_POINT('Ctrl Pts',(17.8723898801252,21.1454760000262,16.6361026834803));
#190662=CARTESIAN_POINT('Ctrl Pts',(17.9217075117375,21.1666969277956,16.6396525695417));
#190663=CARTESIAN_POINT('Ctrl Pts',(18.0061492647197,21.1992855884015,16.645587353291));
#190664=CARTESIAN_POINT('Ctrl Pts',(18.0408614375712,21.2116512478337,16.6479873919274));
#190665=CARTESIAN_POINT('Ctrl Pts',(18.1208698697374,21.2378204369147,16.6534054472326));
#190666=CARTESIAN_POINT('Ctrl Pts',(18.166344682353,21.2510239785951,16.6564034789483));
#190667=CARTESIAN_POINT('Ctrl Pts',(18.2196941546928,21.2645914524403,16.6597974588999));
#190668=CARTESIAN_POINT('Ctrl Pts',(18.2271712134952,21.2664495715927,16.660270346673));
#190669=CARTESIAN_POINT('Ctrl Pts',(18.2391594373556,21.2693593638258,16.6610239029978));
#190670=CARTESIAN_POINT('Ctrl Pts',(18.2436641187745,21.2704371021254,16.6613060123664));
#190671=CARTESIAN_POINT('Ctrl Pts',(18.251662817074,21.2723230466462,16.6618050379573));
#190672=CARTESIAN_POINT('Ctrl Pts',(18.2551553924461,21.2731371688642,16.6620222910668));
#190673=CARTESIAN_POINT('Ctrl Pts',(18.2625783347428,21.2748475873717,16.6624826519642));
#190674=CARTESIAN_POINT('Ctrl Pts',(18.2665091890719,21.2757415316925,16.6627256241678));
#190675=CARTESIAN_POINT('Ctrl Pts',(18.2771600474854,21.2781317457495,16.6633818261994));
#190676=CARTESIAN_POINT('Ctrl Pts',(18.2838849033741,21.2796064872907,16.6637938384153));
#190677=CARTESIAN_POINT('Ctrl Pts',(18.317749162965,21.2868598630743,16.6658575511443));
#190678=CARTESIAN_POINT('Ctrl Pts',(18.3449945059042,21.2921376271542,16.6674822598694));
#190679=CARTESIAN_POINT('Ctrl Pts',(18.4247168713605,21.305960395674,16.6721534260782));
#190680=CARTESIAN_POINT('Ctrl Pts',(18.4774237807726,21.3130667281444,16.6751379419198));
#190681=CARTESIAN_POINT('Ctrl Pts',(18.6704687303813,21.3317240874825,16.6858684342286));
#190682=CARTESIAN_POINT('Ctrl Pts',(18.811594194508,21.3312566479023,16.6933519748958));
#190683=CARTESIAN_POINT('Ctrl Pts',(19.0430318898356,21.3073376209347,16.7062220314881));
#190684=CARTESIAN_POINT('Ctrl Pts',(19.1337093392212,21.2919520849106,16.7114143684209));
#190685=CARTESIAN_POINT('Ctrl Pts',(19.2364859219334,21.2675471915215,16.7176070959298));
#190686=CARTESIAN_POINT('Ctrl Pts',(19.2498461555622,21.264236757693,16.7184180606212));
#190687=CARTESIAN_POINT('Ctrl Pts',(19.2712107174565,21.2587213083957,16.7197248455258));
#190688=CARTESIAN_POINT('Ctrl Pts',(19.2792361441767,21.256599045731,16.7202179933901));
#190689=CARTESIAN_POINT('Ctrl Pts',(19.2934579135764,21.2527485697684,16.7210960034869));
#190690=CARTESIAN_POINT('Ctrl Pts',(19.2996592840608,21.2510392035841,16.7214802498331));
#190691=CARTESIAN_POINT('Ctrl Pts',(19.3125582924535,21.2474203412335,16.7222824353548));
#190692=CARTESIAN_POINT('Ctrl Pts',(19.3192544820815,21.2455060072057,16.7227005281973));
#190693=CARTESIAN_POINT('Ctrl Pts',(19.3366078332922,21.2404521994704,16.7237883953779));
#190694=CARTESIAN_POINT('Ctrl Pts',(19.3472498419153,21.2372618425813,16.7244598248488));
#190695=CARTESIAN_POINT('Ctrl Pts',(19.3932465779149,21.2230769808748,16.7273808314691));
#190696=CARTESIAN_POINT('Ctrl Pts',(19.4283328473901,21.211240348809,16.7296578649472));
#190697=CARTESIAN_POINT('Ctrl Pts',(19.5206065862157,21.1773907392149,16.7357809755207));
#190698=CARTESIAN_POINT('Ctrl Pts',(19.5771763743947,21.1538059500415,16.7396759623199));
#190699=CARTESIAN_POINT('Ctrl Pts',(19.7735699908022,21.061732250791,16.7536842802609));
#190700=CARTESIAN_POINT('Ctrl Pts',(19.9067696523316,20.9803278550712,16.764129980957));
#190701=CARTESIAN_POINT('Ctrl Pts',(20.0425160994926,20.8752510856814,16.775289953845));
#190702=CARTESIAN_POINT('Ctrl Pts',(20.0550829503678,20.8652931775248,16.7763279658382));
#190703=CARTESIAN_POINT('Ctrl Pts',(20.1049344442333,20.8248607370822,16.7804617133952));
#190704=CARTESIAN_POINT('Ctrl Pts',(20.1412906942533,20.7932583288355,16.7835131409363));
#190705=CARTESIAN_POINT('Ctrl Pts',(20.1822126353908,20.7551597162058,16.7869607241291));
#190706=CARTESIAN_POINT('Ctrl Pts',(20.1878561349835,20.7498474289041,16.7874364685001));
#190707=CARTESIAN_POINT('Ctrl Pts',(20.1968353279329,20.7413017289243,16.7881936921878));
#190708=CARTESIAN_POINT('Ctrl Pts',(20.200189711718,20.7380881796405,16.7884766341143));
#190709=CARTESIAN_POINT('Ctrl Pts',(20.2061162129768,20.7323729749374,16.7889766018864));
#190710=CARTESIAN_POINT('Ctrl Pts',(20.2086925803809,20.7298757906693,16.7891939691256));
#190711=CARTESIAN_POINT('Ctrl Pts',(20.2141446022139,20.7245643841674,16.7896539863386));
#190712=CARTESIAN_POINT('Ctrl Pts',(20.2170185800709,20.7217485165535,16.7898965037252));
#190713=CARTESIAN_POINT('Ctrl Pts',(20.2247636935695,20.7141166060536,16.790550189983));
#190714=CARTESIAN_POINT('Ctrl Pts',(20.229619559553,20.7092850387931,16.7909601571455));
#190715=CARTESIAN_POINT('Ctrl Pts',(20.2537291333173,20.6850621027084,16.7929968607804));
#190716=CARTESIAN_POINT('Ctrl Pts',(20.2726305374248,20.6653218181132,16.7945974445035));
#190717=CARTESIAN_POINT('Ctrl Pts',(20.3263480706006,20.6070002168663,16.7991773014619));
#190718=CARTESIAN_POINT('Ctrl Pts',(20.3601341123824,20.5674945862847,16.8020974820705));
#190719=CARTESIAN_POINT('Ctrl Pts',(20.478758729307,20.417978218912,16.8126674599353));
#190720=CARTESIAN_POINT('Ctrl Pts',(20.5541676236854,20.3009411253167,16.8200533415536));
#190721=CARTESIAN_POINT('Ctrl Pts',(20.6610705710436,20.092571824974,16.8329863507533));
#190722=CARTESIAN_POINT('Ctrl Pts',(20.6987904790488,20.0049552655127,16.8383624153762));
#190723=CARTESIAN_POINT('Ctrl Pts',(20.735086711388,19.9020375608247,16.844759331942));
#190724=CARTESIAN_POINT('Ctrl Pts',(20.7395660722882,19.8889274688676,16.8455755240188));
#190725=CARTESIAN_POINT('Ctrl Pts',(20.7465313976245,19.8678681178285,16.8468891268809));
#190726=CARTESIAN_POINT('Ctrl Pts',(20.7490997357537,19.8599463788213,16.8473838201566));
#190727=CARTESIAN_POINT('Ctrl Pts',(20.753570210642,19.8458752594715,16.8482636107686));
#190728=CARTESIAN_POINT('Ctrl Pts',(20.7554911773017,19.8397319376968,16.8486480836222));
#190729=CARTESIAN_POINT('Ctrl Pts',(20.759428708455,19.8269349673162,16.8494497650739));
#190730=CARTESIAN_POINT('Ctrl Pts',(20.761440569367,19.8202799626503,16.8498671224901));
#190731=CARTESIAN_POINT('Ctrl Pts',(20.7665666279569,19.8030170007673,16.8509509528514));
#190732=CARTESIAN_POINT('Ctrl Pts',(20.7696305459446,19.792394443933,16.8516190579823));
#190733=CARTESIAN_POINT('Ctrl Pts',(20.7824568424691,19.7465812201874,16.8545058825182));
#190734=CARTESIAN_POINT('Ctrl Pts',(20.7913904592462,19.7111668886165,16.8567512686278));
#190735=CARTESIAN_POINT('Ctrl Pts',(20.8125908938157,19.6169072666622,16.8627677048293));
#190736=CARTESIAN_POINT('Ctrl Pts',(20.8232747011317,19.5577434073214,16.8665855784685));
#190737=CARTESIAN_POINT('Ctrl Pts',(20.8540465067234,19.3330236263938,16.8812213746667));
#190738=CARTESIAN_POINT('Ctrl Pts',(20.8570717085548,19.1657621641039,16.8924428367485));
#190739=CARTESIAN_POINT('Ctrl Pts',(20.8350135869871,18.9456702212581,16.9067490150706));
#190740=CARTESIAN_POINT('Ctrl Pts',(20.8274881582066,18.8916781997032,16.9102151942044));
#190741=CARTESIAN_POINT('Ctrl Pts',(20.8163427134714,18.8294051445217,16.9141180341984));
#190742=CARTESIAN_POINT('Ctrl Pts',(20.8147450813297,18.8207875928471,16.9146559826978));
#190743=CARTESIAN_POINT('Ctrl Pts',(20.8122475798632,18.8077678327293,16.9154652414464));
#190744=CARTESIAN_POINT('Ctrl Pts',(20.8113871603971,18.8033582815667,16.915738714241));
#190745=CARTESIAN_POINT('Ctrl Pts',(20.8098189048571,18.7954550803654,16.9162277245389));
#190746=CARTESIAN_POINT('Ctrl Pts',(20.8091162795078,18.7919604635481,16.9164435534477));
#190747=CARTESIAN_POINT('Ctrl Pts',(20.8075720175998,18.784378976305,16.9169109149297));
#190748=CARTESIAN_POINT('Ctrl Pts',(20.8067271268241,18.7802928274928,16.917162259105));
#190749=CARTESIAN_POINT('Ctrl Pts',(20.8043242462623,18.7688425942054,16.9178651108676));
#190750=CARTESIAN_POINT('Ctrl Pts',(20.8027390369547,18.7614841971655,16.91831508965));
#190751=CARTESIAN_POINT('Ctrl Pts',(20.7931189259515,18.7179574644438,16.9209675675613));
#190752=CARTESIAN_POINT('Ctrl Pts',(20.7841743813364,18.6819942569394,16.9231212376629));
#190753=CARTESIAN_POINT('Ctrl Pts',(20.7518830240575,18.5653276602424,16.9300381770224));
#190754=CARTESIAN_POINT('Ctrl Pts',(20.7246760644106,18.485771968048,16.9346463484564));
#190755=CARTESIAN_POINT('Ctrl Pts',(20.624603497871,18.2416466683001,16.9490128152082));
#190756=CARTESIAN_POINT('Ctrl Pts',(20.5354830636128,18.0846431388546,16.9586593033433));
#190757=CARTESIAN_POINT('Ctrl Pts',(20.4140080002074,17.9226774527702,16.9704278643016));
#190758=CARTESIAN_POINT('Ctrl Pts',(20.4001305797781,17.9047799958198,16.9717549303042));
#190759=CARTESIAN_POINT('Ctrl Pts',(20.380034776555,17.879704178865,16.9736541721479));
#190760=CARTESIAN_POINT('Ctrl Pts',(20.3740508124741,17.8723393346163,16.9742169841273));
#190761=CARTESIAN_POINT('Ctrl Pts',(20.3642304058494,17.8604174201315,16.9751363389146));
#190762=CARTESIAN_POINT('Ctrl Pts',(20.3604238461326,17.8558358207159,16.975491667119));
#190763=CARTESIAN_POINT('Ctrl Pts',(20.3524014206963,17.8462624676364,16.9762384161879));
#190764=CARTESIAN_POINT('Ctrl Pts',(20.3481816859415,17.8412740514836,16.9766299933147));
#190765=CARTESIAN_POINT('Ctrl Pts',(20.3380621118027,17.8294227679942,16.9775662377315));
#190766=CARTESIAN_POINT('Ctrl Pts',(20.3321412602634,17.822578084736,16.9781117698801));
#190767=CARTESIAN_POINT('Ctrl Pts',(20.3119201134858,17.7995025498768,16.9799674600976));
#190768=CARTESIAN_POINT('Ctrl Pts',(20.2974153672065,17.7834534083499,16.9812861371627));
#190769=CARTESIAN_POINT('Ctrl Pts',(20.2162434483324,17.6963597958894,16.98860094668));
#190770=CARTESIAN_POINT('Ctrl Pts',(20.1449878787224,17.6297696927172,16.994795233597));
#190771=CARTESIAN_POINT('Ctrl Pts',(19.9646963641727,17.4832017145389,17.0099096971113));
#190772=CARTESIAN_POINT('Ctrl Pts',(19.8520898680962,17.4082873325656,17.0189377606499));
#190773=CARTESIAN_POINT('Ctrl Pts',(19.673575503724,17.3127247438807,17.0321304690865));
#190774=CARTESIAN_POINT('Ctrl Pts',(19.6125298070876,17.2837121742191,17.0364595397366));
#190775=CARTESIAN_POINT('Ctrl Pts',(19.5416245342323,17.2540845962664,17.0412040168048));
#190776=CARTESIAN_POINT('Ctrl Pts',(19.533030003088,17.2505596548048,17.0417744639915));
#190777=CARTESIAN_POINT('Ctrl Pts',(19.5202008942851,17.2453963361491,17.0426187874855));
#190778=CARTESIAN_POINT('Ctrl Pts',(19.5159839312644,17.2437148804379,17.0428951690419));
#190779=CARTESIAN_POINT('Ctrl Pts',(19.5084429393208,17.2407360924661,17.0433873153194));
#190780=CARTESIAN_POINT('Ctrl Pts',(19.5051210184411,17.2394335904819,17.0436033876423));
#190781=CARTESIAN_POINT('Ctrl Pts',(19.4979393851144,17.2366386501435,17.0440689404596));
#190782=CARTESIAN_POINT('Ctrl Pts',(19.494078597153,17.2351491324597,17.0443182450771));
#190783=CARTESIAN_POINT('Ctrl Pts',(19.4833303712375,17.231038560833,17.0450096590298));
#190784=CARTESIAN_POINT('Ctrl Pts',(19.4764335009835,17.228442105236,17.0454503187627));
#190785=CARTESIAN_POINT('Ctrl Pts',(19.4372004693585,17.2139055405397,17.0479407600401));
#190786=CARTESIAN_POINT('Ctrl Pts',(19.4045880380314,17.202719847369,17.0499484041586));
#190787=CARTESIAN_POINT('Ctrl Pts',(19.3006675955519,17.1698904206573,17.0561926336432));
#190788=CARTESIAN_POINT('Ctrl Pts',(19.2284791510635,17.1512105553931,17.0603066919223));
#190789=CARTESIAN_POINT('Ctrl Pts',(18.964904718397,17.0976665462423,17.0749992300359));
#190790=CARTESIAN_POINT('Ctrl Pts',(18.7699560274011,17.0853948146125,17.0853523920085));
#190791=CARTESIAN_POINT('Ctrl Pts',(18.5550373548284,17.10147248897,17.0979001947344));
#190792=CARTESIAN_POINT('Ctrl Pts',(18.5340276179722,17.1033603374155,17.0991376021045));
#190793=CARTESIAN_POINT('Ctrl Pts',(18.5048014842644,17.1064273996779,17.1008752684889));
#190794=CARTESIAN_POINT('Ctrl Pts',(18.496558077905,17.1073414915208,17.1013672014366));
#190795=CARTESIAN_POINT('Ctrl Pts',(18.4823262254644,17.1090043455886,17.1022197185278));
#190796=CARTESIAN_POINT('Ctrl Pts',(18.4763351774992,17.1097303223911,17.1025795813548));
#190797=CARTESIAN_POINT('Ctrl Pts',(18.4639237946304,17.1112881732013,17.1033271738693));
#190798=CARTESIAN_POINT('Ctrl Pts',(18.4575040148025,17.1121239005052,17.103715021666));
#190799=CARTESIAN_POINT('Ctrl Pts',(18.4424577301492,17.114152856131,17.1046267920114));
#190800=CARTESIAN_POINT('Ctrl Pts',(18.4338346022621,17.1153698870456,17.1051514623112));
#190801=CARTESIAN_POINT('Ctrl Pts',(18.4057712341489,17.1195073925186,17.1068660343564));
#190802=CARTESIAN_POINT('Ctrl Pts',(18.3863645598273,17.1226453821957,17.1080627934563));
#190803=CARTESIAN_POINT('Ctrl Pts',(18.2867785682032,17.1401746396328,17.1142628546294));
#190804=CARTESIAN_POINT('Ctrl Pts',(18.207443565215,17.1589131869396,17.1194029667741));
#190805=CARTESIAN_POINT('Ctrl Pts',(17.9776814634974,17.227384209843,17.1348669479345));
#190806=CARTESIAN_POINT('Ctrl Pts',(17.8315362136191,17.2894636750079,17.1454942249207));
#190807=CARTESIAN_POINT('Ctrl Pts',(17.6386458723129,17.3982998841389,17.1598922888129));
#190808=CARTESIAN_POINT('Ctrl Pts',(17.5850214087633,17.4318057485674,17.1639327519656));
#190809=CARTESIAN_POINT('Ctrl Pts',(17.5254014008468,17.4728794815531,17.1684018676483));
#190810=CARTESIAN_POINT('Ctrl Pts',(17.5178649502775,17.4781442476707,17.1689663448772));
#190811=CARTESIAN_POINT('Ctrl Pts',(17.5066738915779,17.4860709986418,17.169803577061));
#190812=CARTESIAN_POINT('Ctrl Pts',(17.5029932433529,17.4886957870032,17.1700787773126));
#190813=CARTESIAN_POINT('Ctrl Pts',(17.496506876361,17.4933528387723,17.1705634374976));
#190814=CARTESIAN_POINT('Ctrl Pts',(17.4936977193714,17.4953802126407,17.1707732277142));
#190815=CARTESIAN_POINT('Ctrl Pts',(17.4908825941583,17.4974224221021,17.1709833504218));
#190816=CARTESIAN_POINT('Ctrl Pts',(17.4908716997384,17.4974303255281,17.1709841635864));
#190817=CARTESIAN_POINT('Ctrl Pts',(17.4908500946672,17.4974459993784,17.1709857761959));
#190818=CARTESIAN_POINT('Ctrl Pts',(17.4908393836709,17.4974537700478,17.1709865756665));
#190819=CARTESIAN_POINT('Ctrl Pts',(17.4908181408182,17.4974691817272,17.1709881612336));
#190820=CARTESIAN_POINT('Ctrl Pts',(17.4908076091093,17.4974768226251,17.1709889473191));
#190821=CARTESIAN_POINT('Ctrl Pts',(17.490786721538,17.4974919771359,17.1709905063618));
#190822=CARTESIAN_POINT('Ctrl Pts',(17.4907763655008,17.4974994908707,17.1709912793322));
#190823=CARTESIAN_POINT('Ctrl Pts',(17.4907563393645,17.4975140209408,17.1709927740718));
#190824=CARTESIAN_POINT('Ctrl Pts',(17.4907466691971,17.4975210373074,17.1709934958465));
#190825=CARTESIAN_POINT('Ctrl Pts',(17.4907273644813,17.4975350444458,17.1709949367345));
#190826=CARTESIAN_POINT('Ctrl Pts',(17.4907177303752,17.497542034896,17.170995655815));
#190827=CARTESIAN_POINT('Ctrl Pts',(17.490698498942,17.4975559893572,17.1709970912282));
#190828=CARTESIAN_POINT('Ctrl Pts',(17.4906889011106,17.4975629537333,17.1709978075986));
#190829=CARTESIAN_POINT('Ctrl Pts',(17.4906697409776,17.4975768569501,17.1709992376849));
#190830=CARTESIAN_POINT('Ctrl Pts',(17.490660178835,17.4975837956746,17.170999951389));
#190831=CARTESIAN_POINT('Ctrl Pts',(17.487358510376,17.4999796782725,17.1712463825647));
#190832=CARTESIAN_POINT('Ctrl Pts',(17.4840732641445,17.5023781282419,17.171491437748));
#190833=CARTESIAN_POINT('Ctrl Pts',(17.477282283717,17.5073660672984,17.171997729333));
#190834=CARTESIAN_POINT('Ctrl Pts',(17.4737775886552,17.5099569465248,17.1722588692457));
#190835=CARTESIAN_POINT('Ctrl Pts',(17.4648864425515,17.5165723715022,17.1729210555884));
#190836=CARTESIAN_POINT('Ctrl Pts',(17.4595110734997,17.5206118230398,17.1733211102986));
#190837=CARTESIAN_POINT('Ctrl Pts',(17.4440634507962,17.5323358888336,17.1744702402052));
#190838=CARTESIAN_POINT('Ctrl Pts',(17.4340406358823,17.5400855296944,17.1752151597165));
#190839=CARTESIAN_POINT('Ctrl Pts',(17.399889519129,17.5669844747819,17.1777533680757));
#190840=CARTESIAN_POINT('Ctrl Pts',(17.3761089298929,17.586570914311,17.1795208528137));
#190841=CARTESIAN_POINT('Ctrl Pts',(17.2575602376774,17.6886346155539,17.1883808123201));
#190842=CARTESIAN_POINT('Ctrl Pts',(17.1698348093949,17.7789165765252,17.19511241989));
#190843=CARTESIAN_POINT('Ctrl Pts',(17.0690602118355,17.9030110439496,17.2038141847654));
#190844=CARTESIAN_POINT('Ctrl Pts',(17.0481391182054,17.9300891420151,17.2056822771101));
#190845=CARTESIAN_POINT('Ctrl Pts',(16.9656574075929,18.0423680161385,17.2133427635454));
#190846=CARTESIAN_POINT('Ctrl Pts',(16.9098332437536,18.1315799084601,17.2192442854583));
#190847=CARTESIAN_POINT('Ctrl Pts',(16.8543055473955,18.2370204989898,17.2262274650637));
#190848=CARTESIAN_POINT('Ctrl Pts',(16.8478684790826,18.2495452818439,17.2270568985404));
#190849=CARTESIAN_POINT('Ctrl Pts',(16.8377945246964,18.269637020233,17.2283877586346));
#190850=CARTESIAN_POINT('Ctrl Pts',(16.8340767980751,18.2771631363358,17.2288863517731));
#190851=CARTESIAN_POINT('Ctrl Pts',(16.8275830681521,18.2905082582108,17.2297706527729));
#190852=CARTESIAN_POINT('Ctrl Pts',(16.8247886863266,18.2963182394621,17.2301557144048));
#190853=CARTESIAN_POINT('Ctrl Pts',(16.8190486272531,18.3083936780619,17.23095620865));
#190854=CARTESIAN_POINT('Ctrl Pts',(16.816107062717,18.3146609950827,17.231371778131));
#190855=CARTESIAN_POINT('Ctrl Pts',(16.8086037967711,18.3308535466727,17.2324457831657));
#190856=CARTESIAN_POINT('Ctrl Pts',(16.804088118517,18.3407997693523,17.2331057955402));
#190857=CARTESIAN_POINT('Ctrl Pts',(16.7852989170205,18.3830504873978,17.2359110825272));
#190858=CARTESIAN_POINT('Ctrl Pts',(16.7717586557371,18.4156730375422,17.2380811902301));
#190859=CARTESIAN_POINT('Ctrl Pts',(16.7383836134081,18.5021313866184,17.2438466495949));
#190860=CARTESIAN_POINT('Ctrl Pts',(16.7199110919727,18.5564586143804,17.2474841213431));
#190861=CARTESIAN_POINT('Ctrl Pts',(16.6461257273694,18.8063336336557,17.2642610289432));
#190862=CARTESIAN_POINT('Ctrl Pts',(16.616945001367,19.0084357473791,17.2780828555683));
#190863=CARTESIAN_POINT('Ctrl Pts',(16.6170000778107,19.2115739777624,17.2909082101745));
#190864=CARTESIAN_POINT('Ctrl Pts',(16.617000078448,19.2115763236151,17.2909083582825));
#190865=CARTESIAN_POINT('Ctrl Pts',(16.6170043638434,19.2273177950194,17.2919022126078));
#190866=CARTESIAN_POINT('Ctrl Pts',(16.6171842237099,19.2430592943021,17.2928889421261));
#190867=CARTESIAN_POINT('Ctrl Pts',(16.6177851449818,19.2696677192771,17.2945431885913));
#190868=CARTESIAN_POINT('Ctrl Pts',(16.6181143695731,19.2805357749806,17.2952150009985));
#190869=CARTESIAN_POINT('Ctrl Pts',(16.6187085001659,19.2961682425581,17.2961753174121));
#190870=CARTESIAN_POINT('Ctrl Pts',(16.6189057980453,19.3009348467959,17.2964673297887));
#190871=CARTESIAN_POINT('Ctrl Pts',(16.619279118516,19.3092719287477,17.2969766219361));
#190872=CARTESIAN_POINT('Ctrl Pts',(16.6194480741323,19.312842681655,17.2971942834138));
#190873=CARTESIAN_POINT('Ctrl Pts',(16.6197955281192,19.3198119123319,17.297618170331));
#190874=CARTESIAN_POINT('Ctrl Pts',(16.6199731786469,19.323210429224,17.297824442496));
#190875=CARTESIAN_POINT('Ctrl Pts',(16.6203449444749,19.3300079695181,17.298236131484));
#190876=CARTESIAN_POINT('Ctrl Pts',(16.6205390638766,19.3334069541103,17.2984415483144));
#190877=CARTESIAN_POINT('Ctrl Pts',(16.6210263182197,19.3415917677725,17.2989351657796));
#190878=CARTESIAN_POINT('Ctrl Pts',(16.6213275158841,19.3463771235785,17.2992229173022));
#190879=CARTESIAN_POINT('Ctrl Pts',(16.6224923796179,19.3639326315363,17.3002755809276));
#190880=CARTESIAN_POINT('Ctrl Pts',(16.6234556133261,19.3766961998604,17.3010351247462));
#190881=CARTESIAN_POINT('Ctrl Pts',(16.6267051711631,19.415109240068,17.3033056984767));
#190882=CARTESIAN_POINT('Ctrl Pts',(16.629343841443,19.4407273490183,17.3047993510392));
#190883=CARTESIAN_POINT('Ctrl Pts',(16.6408529428832,19.5354696449089,17.3102675854388));
#190884=CARTESIAN_POINT('Ctrl Pts',(16.6526677492806,19.6041954381617,17.314124798583));
#190885=CARTESIAN_POINT('Ctrl Pts',(16.6879369732018,19.7621933541582,17.3229825713365));
#190886=CARTESIAN_POINT('Ctrl Pts',(16.7138584209825,19.8506750620402,17.3279387938027));
#190887=CARTESIAN_POINT('Ctrl Pts',(16.7454194652257,19.9371104989717,17.3329785907215));
#190888=CARTESIAN_POINT('Origin',(18.734,19.211,0.));
#190889=CARTESIAN_POINT('',(16.7454193519082,19.9371101886317,18.3568545479166));
#190890=CARTESIAN_POINT('',(16.7454193782244,19.9371102607032,18.1318062886951));
#190891=CARTESIAN_POINT('',(16.7454193623258,19.9371102171621,0.));
#190892=CARTESIAN_POINT('Ctrl Pts',(16.7454193519082,19.9371101886317,18.3568545479166));
#190893=CARTESIAN_POINT('Ctrl Pts',(16.740076494339,19.9224778320914,18.3558520679459));
#190894=CARTESIAN_POINT('Ctrl Pts',(16.7348945232057,19.9077848210586,18.3548454931849));
#190895=CARTESIAN_POINT('Ctrl Pts',(16.6860061867035,19.7641286466884,18.3450068997072));
#190896=CARTESIAN_POINT('Ctrl Pts',(16.6546780663117,19.6312935582155,18.3359031838316));
#190897=CARTESIAN_POINT('Ctrl Pts',(16.6262469231319,19.4223145563828,18.322121638853));
#190898=CARTESIAN_POINT('Ctrl Pts',(16.6200989586563,19.3477543266621,18.3173148259657));
#190899=CARTESIAN_POINT('Ctrl Pts',(16.617649086585,19.2641628394303,18.3121557615785));
#190900=CARTESIAN_POINT('Ctrl Pts',(16.6174451484744,19.2553062410246,18.3116120546279));
#190901=CARTESIAN_POINT('Ctrl Pts',(16.6172222392365,19.2419958500716,18.3107995510631));
#190902=CARTESIAN_POINT('Ctrl Pts',(16.6171617203538,19.2375429811444,18.3105285125938));
#190903=CARTESIAN_POINT('Ctrl Pts',(16.6170816556437,19.2298703476926,18.3100628702711));
#190904=CARTESIAN_POINT('Ctrl Pts',(16.61705540401,19.226650708558,18.309867894064));
#190905=CARTESIAN_POINT('Ctrl Pts',(16.6170125976616,19.2193608843705,18.3094273900038));
#190906=CARTESIAN_POINT('Ctrl Pts',(16.6170004354123,19.2152907137506,18.3091821108928));
#190907=CARTESIAN_POINT('Ctrl Pts',(16.6169992761201,19.2041601536932,18.3085131255452));
#190908=CARTESIAN_POINT('Ctrl Pts',(16.6170338608298,19.197099740555,18.308090719101));
#190909=CARTESIAN_POINT('Ctrl Pts',(16.6174008058345,19.160040260732,18.3058831615146));
#190910=CARTESIAN_POINT('Ctrl Pts',(16.6183355228245,19.1300489516173,18.3041297092626));
#190911=CARTESIAN_POINT('Ctrl Pts',(16.6230423579442,19.0403336687759,18.298956773104));
#190912=CARTESIAN_POINT('Ctrl Pts',(16.6287092855466,18.9807366743784,18.2956161886736));
#190913=CARTESIAN_POINT('Ctrl Pts',(16.6597465945341,18.7559400282549,18.2831216772672));
#190914=CARTESIAN_POINT('Ctrl Pts',(16.7021118177646,18.593717083346,18.2742743143245));
#190915=CARTESIAN_POINT('Ctrl Pts',(16.7847366131576,18.3830080322236,18.2615097650854));
#190916=CARTESIAN_POINT('Ctrl Pts',(16.8086669963622,18.3287923457201,18.2581084204706));
#190917=CARTESIAN_POINT('Ctrl Pts',(16.8402461663869,18.2646727461113,18.2539094734308));
#190918=CARTESIAN_POINT('Ctrl Pts',(16.845749831968,18.2537382033796,18.2531870918306));
#190919=CARTESIAN_POINT('Ctrl Pts',(16.8549745051634,18.2357999819467,18.2519912824719));
#190920=CARTESIAN_POINT('Ctrl Pts',(16.8586406319954,18.2287682943024,18.2515197857228));
#190921=CARTESIAN_POINT('Ctrl Pts',(16.8653239031246,18.2161234984386,18.2506668736345));
#190922=CARTESIAN_POINT('Ctrl Pts',(16.868327061841,18.2105030760462,18.250285957569));
#190923=CARTESIAN_POINT('Ctrl Pts',(16.8748002290214,18.1985190135426,18.2494698382465));
#190924=CARTESIAN_POINT('Ctrl Pts',(16.8782776275804,18.1921594772435,18.2490343747704));
#190925=CARTESIAN_POINT('Ctrl Pts',(16.8877882533566,18.1749764805655,18.2478512605664));
#190926=CARTESIAN_POINT('Ctrl Pts',(16.8938838922957,18.1641880559534,18.2471013779622));
#190927=CARTESIAN_POINT('Ctrl Pts',(16.9256762180647,18.1090559138824,18.2432322935626));
#190928=CARTESIAN_POINT('Ctrl Pts',(16.9528805237454,18.065605584064,18.2400586925772));
#190929=CARTESIAN_POINT('Ctrl Pts',(17.0774365498924,17.8818493423726,18.226076661577));
#190930=CARTESIAN_POINT('Ctrl Pts',(17.1899788020233,17.7526358939629,18.2147047222254));
#190931=CARTESIAN_POINT('Ctrl Pts',(17.3851544770935,17.5767493254368,18.197426436311));
#190932=CARTESIAN_POINT('Ctrl Pts',(17.4574777109291,17.5196530990333,18.1914503969016));
#190933=CARTESIAN_POINT('Ctrl Pts',(17.5412586688597,17.4619572346241,18.1851656251151));
#190934=CARTESIAN_POINT('Ctrl Pts',(17.5492592078464,17.4565280732736,18.1845715864903));
#190935=CARTESIAN_POINT('Ctrl Pts',(17.56113269998,17.4485889841799,18.1836993116582));
#190936=CARTESIAN_POINT('Ctrl Pts',(17.5649769841914,17.4460366911517,18.1834183268371));
#190937=CARTESIAN_POINT('Ctrl Pts',(17.5718145274698,17.4415292573937,18.1829211401122));
#190938=CARTESIAN_POINT('Ctrl Pts',(17.5748044214367,17.4395691114763,18.1827046050697));
#190939=CARTESIAN_POINT('Ctrl Pts',(17.5812240312247,17.4353836901448,18.1822415595434));
#190940=CARTESIAN_POINT('Ctrl Pts',(17.5846552220479,17.4331607789077,18.1819952064571));
#190941=CARTESIAN_POINT('Ctrl Pts',(17.594098515162,17.4270816667536,18.1813202541874));
#190942=CARTESIAN_POINT('Ctrl Pts',(17.6001237909021,17.4232458892285,18.1808929939474));
#190943=CARTESIAN_POINT('Ctrl Pts',(17.6325054999265,17.4028607917225,18.1786142275692));
#190944=CARTESIAN_POINT('Ctrl Pts',(17.6592065247687,17.3868627389999,18.1767968998646));
#190945=CARTESIAN_POINT('Ctrl Pts',(17.8286695720217,17.2903416613725,18.1655816897482));
#190946=CARTESIAN_POINT('Ctrl Pts',(17.9800402574271,17.2260292886871,18.1569209865215));
#190947=CARTESIAN_POINT('Ctrl Pts',(18.2497879317054,17.1467893202156,18.1415316130463));
#190948=CARTESIAN_POINT('Ctrl Pts',(18.364779749836,17.1231546591343,18.1349895556366));
#190949=CARTESIAN_POINT('Ctrl Pts',(18.4953200969613,17.1074493715658,18.1272869662159));
#190950=CARTESIAN_POINT('Ctrl Pts',(18.5095292559827,17.1058857008095,18.1264451712769));
#190951=CARTESIAN_POINT('Ctrl Pts',(18.5321672416965,17.1036262685549,18.1250982179376));
#190952=CARTESIAN_POINT('Ctrl Pts',(18.5405864376635,17.1028368903122,18.1245960033195));
#190953=CARTESIAN_POINT('Ctrl Pts',(18.5554424107499,17.1015337449926,18.123707492998));
#190954=CARTESIAN_POINT('Ctrl Pts',(18.5618772684991,17.1009989437043,18.1233218637923));
#190955=CARTESIAN_POINT('Ctrl Pts',(18.5751908612632,17.0999537583577,18.1225223688771));
#190956=CARTESIAN_POINT('Ctrl Pts',(18.5820698377484,17.0994475377237,18.1221083770503));
#190957=CARTESIAN_POINT('Ctrl Pts',(18.5997320092373,17.0982345414584,18.1210430584122));
#190958=CARTESIAN_POINT('Ctrl Pts',(18.6105182665399,17.0975767033387,18.1203902031609));
#190959=CARTESIAN_POINT('Ctrl Pts',(18.6555453165899,17.0951764432361,18.1176551189331));
#190960=CARTESIAN_POINT('Ctrl Pts',(18.6898192893575,17.0941834492349,18.1155495794422));
#190961=CARTESIAN_POINT('Ctrl Pts',(18.7791606206309,17.0937656782698,18.1099963604658));
#190962=CARTESIAN_POINT('Ctrl Pts',(18.8342054556308,17.0956563630508,18.1065103172253));
#190963=CARTESIAN_POINT('Ctrl Pts',(18.998174968728,17.1077026260574,18.0959427836498));
#190964=CARTESIAN_POINT('Ctrl Pts',(19.1064471912572,17.1241536040697,18.0887128958368));
#190965=CARTESIAN_POINT('Ctrl Pts',(19.2565114809359,17.1590082109158,18.0785361081056));
#190966=CARTESIAN_POINT('Ctrl Pts',(19.2997378818415,17.17050266466,18.0755875793002));
#190967=CARTESIAN_POINT('Ctrl Pts',(19.3667238994199,17.190607586601,18.0710173663246));
#190968=CARTESIAN_POINT('Ctrl Pts',(19.3907483694794,17.1982887223917,18.0693781228253));
#190969=CARTESIAN_POINT('Ctrl Pts',(19.4618604547071,17.222433685406,18.0645357795359));
#190970=CARTESIAN_POINT('Ctrl Pts',(19.5085132254562,17.2401354792261,18.0613717201597));
#190971=CARTESIAN_POINT('Ctrl Pts',(19.5617049774984,17.2624994109848,18.0578132630285));
#190972=CARTESIAN_POINT('Ctrl Pts',(19.5688924915254,17.2655682723176,18.0573334910496));
#190973=CARTESIAN_POINT('Ctrl Pts',(19.5803423212537,17.2705321620781,18.0565710998989));
#190974=CARTESIAN_POINT('Ctrl Pts',(19.5846155746587,17.2724015630198,18.0562869871464));
#190975=CARTESIAN_POINT('Ctrl Pts',(19.5921673990151,17.2757350034144,18.0557856904529));
#190976=CARTESIAN_POINT('Ctrl Pts',(19.5954484665941,17.2771932795947,18.055568158783));
#190977=CARTESIAN_POINT('Ctrl Pts',(19.6023887666971,17.2802990771642,18.0551086066885));
#190978=CARTESIAN_POINT('Ctrl Pts',(19.6060470222461,17.281948654086,18.0548667147028));
#190979=CARTESIAN_POINT('Ctrl Pts',(19.6158937415444,17.2864224616233,18.054216485923));
#190980=CARTESIAN_POINT('Ctrl Pts',(19.6220733808811,17.289266161603,18.0538093291238));
#190981=CARTESIAN_POINT('Ctrl Pts',(19.6524929943149,17.3034425000545,18.0518090906745));
#190982=CARTESIAN_POINT('Ctrl Pts',(19.6765314979828,17.3152047783861,18.0502410513488));
#190983=CARTESIAN_POINT('Ctrl Pts',(19.7451552828336,17.3504111613286,18.0457830748306));
#190984=CARTESIAN_POINT('Ctrl Pts',(19.7891371305345,17.3749956032445,18.0429485404463));
#190985=CARTESIAN_POINT('Ctrl Pts',(19.9451388821755,17.4696550482877,18.0328294029101));
#190986=CARTESIAN_POINT('Ctrl Pts',(20.0514153025267,17.548604440817,18.0257921617174));
#190987=CARTESIAN_POINT('Ctrl Pts',(20.2269410679448,17.7064655857836,18.0128055916103));
#190988=CARTESIAN_POINT('Ctrl Pts',(20.2990038251029,17.7815750039524,18.0069651109322));
#190989=CARTESIAN_POINT('Ctrl Pts',(20.3742143762197,17.8724995571169,18.000050190486));
#190990=CARTESIAN_POINT('Ctrl Pts',(20.3830665550343,17.8834209558686,17.9992221360428));
#190991=CARTESIAN_POINT('Ctrl Pts',(20.3970252909831,17.9009976222521,17.9978930722773));
#190992=CARTESIAN_POINT('Ctrl Pts',(20.4022022975667,17.9075965937368,17.9973948842505));
#190993=CARTESIAN_POINT('Ctrl Pts',(20.411288395844,17.919321174687,17.9965110528354));
#190994=CARTESIAN_POINT('Ctrl Pts',(20.4152135692636,17.9244342287701,17.9961260534136));
#190995=CARTESIAN_POINT('Ctrl Pts',(20.4233078228384,17.9350783515179,17.995325441143));
#190996=CARTESIAN_POINT('Ctrl Pts',(20.4274732275811,17.9406121068507,17.9949096902034));
#190997=CARTESIAN_POINT('Ctrl Pts',(20.438145688577,17.9549362736984,17.9938346874009));
#190998=CARTESIAN_POINT('Ctrl Pts',(20.4446118559668,17.9637567664559,17.9931738531268));
#190999=CARTESIAN_POINT('Ctrl Pts',(20.4717390818637,18.0013687726289,17.9903603920129));
#191000=CARTESIAN_POINT('Ctrl Pts',(20.4917428545349,18.0306252112488,17.9881827514338));
#191001=CARTESIAN_POINT('Ctrl Pts',(20.5423272094405,18.108746233145,17.9823923506699));
#191002=CARTESIAN_POINT('Ctrl Pts',(20.5716613084003,18.1583791528563,17.9787370157447));
#191003=CARTESIAN_POINT('Ctrl Pts',(20.6747923302676,18.3503551352019,17.9647013992251));
#191004=CARTESIAN_POINT('Ctrl Pts',(20.7343605191413,18.499708991169,17.9539398307783));
#191005=CARTESIAN_POINT('Ctrl Pts',(20.7802600837489,18.6681255173914,17.9425861667266));
#191006=CARTESIAN_POINT('Ctrl Pts',(20.7838765009978,18.6819448244828,17.9416604713825));
#191007=CARTESIAN_POINT('Ctrl Pts',(20.7892582138368,18.7033938796504,17.9402338167324));
#191008=CARTESIAN_POINT('Ctrl Pts',(20.7911214725792,18.7109984513307,17.9397299691526));
#191009=CARTESIAN_POINT('Ctrl Pts',(20.80304652801,18.7608637340246,17.9364396271177));
#191010=CARTESIAN_POINT('Ctrl Pts',(20.8118484655297,18.8034186662922,17.9336950004071));
#191011=CARTESIAN_POINT('Ctrl Pts',(20.8206295294387,18.8536169637691,17.9305542994598));
#191012=CARTESIAN_POINT('Ctrl Pts',(20.821884531409,18.8610234078396,17.9300933683794));
#191013=CARTESIAN_POINT('Ctrl Pts',(20.8238483803386,18.8729998063972,17.929352174678));
#191014=CARTESIAN_POINT('Ctrl Pts',(20.8245817101916,18.8775656022116,17.9290705782175));
#191015=CARTESIAN_POINT('Ctrl Pts',(20.8258556216553,18.8856665601731,17.9285727152734));
#191016=CARTESIAN_POINT('Ctrl Pts',(20.8264022115365,18.8892007228718,17.9283561122643));
#191017=CARTESIAN_POINT('Ctrl Pts',(20.8275535386188,18.8967719871733,17.9278933700577));
#191018=CARTESIAN_POINT('Ctrl Pts',(20.828155554004,18.9008094466465,17.9276473859137));
#191019=CARTESIAN_POINT('Ctrl Pts',(20.8297747227331,18.911888108136,17.926974484709));
#191020=CARTESIAN_POINT('Ctrl Pts',(20.8307680778246,18.9189328101458,17.9265488930767));
#191021=CARTESIAN_POINT('Ctrl Pts',(20.8358632932361,18.9564335439481,17.9242949130991));
#191022=CARTESIAN_POINT('Ctrl Pts',(20.8393373739792,18.9869728837622,17.9224998288459));
#191023=CARTESIAN_POINT('Ctrl Pts',(20.8478187974684,19.0794140115214,17.917159128473));
#191024=CARTESIAN_POINT('Ctrl Pts',(20.8507692325605,19.1414736032094,17.9136985749968));
#191025=CARTESIAN_POINT('Ctrl Pts',(20.8515020647841,19.3504777029911,17.9022076870108));
#191026=CARTESIAN_POINT('Ctrl Pts',(20.836726033996,19.4970296331771,17.894393777087));
#191027=CARTESIAN_POINT('Ctrl Pts',(20.7917426403449,19.7139446565672,17.8820237681741));
#191028=CARTESIAN_POINT('Ctrl Pts',(20.7727375162154,19.7861571054887,17.8777714523651));
#191029=CARTESIAN_POINT('Ctrl Pts',(20.7459588025204,19.8696977498765,17.8726239499246));
#191030=CARTESIAN_POINT('Ctrl Pts',(20.7418402415141,19.8821471535625,17.8718508507838));
#191031=CARTESIAN_POINT('Ctrl Pts',(20.7349598914134,19.9023144657568,17.8705883435627));
#191032=CARTESIAN_POINT('Ctrl Pts',(20.7322684274895,19.9100561253736,17.8701012598875));
#191033=CARTESIAN_POINT('Ctrl Pts',(20.7273954921333,19.9238143996634,17.8692311891521));
#191034=CARTESIAN_POINT('Ctrl Pts',(20.725231555384,19.9298371497625,17.8688487889445));
#191035=CARTESIAN_POINT('Ctrl Pts',(20.7206142430144,19.9425073868644,17.8680410685596));
#191036=CARTESIAN_POINT('Ctrl Pts',(20.7181547393491,19.9491525425025,17.8676155475376));
#191037=CARTESIAN_POINT('Ctrl Pts',(20.7115607172459,19.9666973638918,17.866486982612));
#191038=CARTESIAN_POINT('Ctrl Pts',(20.7073694928482,19.9775753272612,17.8657820455699));
#191039=CARTESIAN_POINT('Ctrl Pts',(20.6874757396769,20.0279633644001,17.8624919759757));
#191040=CARTESIAN_POINT('Ctrl Pts',(20.6706760015987,20.0670270203303,17.859870065302));
#191041=CARTESIAN_POINT('Ctrl Pts',(20.6211523552231,20.1732491068526,17.8525365727408));
#191042=CARTESIAN_POINT('Ctrl Pts',(20.5860349627057,20.2392178570208,17.847748635772));
#191043=CARTESIAN_POINT('Ctrl Pts',(20.4781659525271,20.4183274708986,17.8341270287711));
#191044=CARTESIAN_POINT('Ctrl Pts',(20.3980195168164,20.5265954937742,17.8251332411692));
#191045=CARTESIAN_POINT('Ctrl Pts',(20.2985350816605,20.6372278452781,17.8154547656744));
#191046=CARTESIAN_POINT('Ctrl Pts',(20.2888085551305,20.6478250622142,17.8145225033542));
#191047=CARTESIAN_POINT('Ctrl Pts',(20.2756203479755,20.661903089272,17.8132778759741));
#191048=CARTESIAN_POINT('Ctrl Pts',(20.2722536162943,20.6654720294137,17.8129618104336));
#191049=CARTESIAN_POINT('Ctrl Pts',(20.2370057730656,20.702577605314,17.8096703805597));
#191050=CARTESIAN_POINT('Ctrl Pts',(20.2040429620984,20.7350749666842,17.8067416687523));
#191051=CARTESIAN_POINT('Ctrl Pts',(20.1644172472134,20.7716582064957,17.8034169227904));
#191052=CARTESIAN_POINT('Ctrl Pts',(20.1587674340117,20.7768177740928,17.8029473428258));
#191053=CARTESIAN_POINT('Ctrl Pts',(20.1496642432143,20.7850409965516,17.8021980355265));
#191054=CARTESIAN_POINT('Ctrl Pts',(20.1462286617711,20.7881241283246,17.8019168924313));
#191055=CARTESIAN_POINT('Ctrl Pts',(20.1401076462442,20.7935811617298,17.8014189573226));
#191056=CARTESIAN_POINT('Ctrl Pts',(20.1374262373114,20.7959595084525,17.8012018336539));
#191057=CARTESIAN_POINT('Ctrl Pts',(20.1317093346962,20.8010043834955,17.8007410599272));
#191058=CARTESIAN_POINT('Ctrl Pts',(20.1286722511425,20.8036690291311,17.8004975489827));
#191059=CARTESIAN_POINT('Ctrl Pts',(20.1204086158847,20.8108775304631,17.7998383653363));
#191060=CARTESIAN_POINT('Ctrl Pts',(20.1151673126897,20.8154045063707,17.7994239292089));
#191061=CARTESIAN_POINT('Ctrl Pts',(20.0884293472343,20.8382702761116,17.7973276717859));
#191062=CARTESIAN_POINT('Ctrl Pts',(20.0665881731456,20.8562040435523,17.7956738720474));
#191063=CARTESIAN_POINT('Ctrl Pts',(20.0014877940827,20.9075105336547,17.7908914905463));
#191064=CARTESIAN_POINT('Ctrl Pts',(19.9572864013886,20.9396539575593,17.7878284188086));
#191065=CARTESIAN_POINT('Ctrl Pts',(19.791190389639,21.0508743040341,17.7767813704655));
#191066=CARTESIAN_POINT('Ctrl Pts',(19.6624951683983,21.1190586362279,17.769066338311));
#191067=CARTESIAN_POINT('Ctrl Pts',(19.4900493056413,21.1888117463425,17.7587442219642));
#191068=CARTESIAN_POINT('Ctrl Pts',(19.4518374871976,21.2029987335442,17.7564601158652));
#191069=CARTESIAN_POINT('Ctrl Pts',(19.3669280580991,21.2317627633867,17.7513661083166));
#191070=CARTESIAN_POINT('Ctrl Pts',(19.3200880239051,21.2458416052626,17.7485438158493));
#191071=CARTESIAN_POINT('Ctrl Pts',(19.2605913014438,21.2614999657773,17.7449256079353));
#191072=CARTESIAN_POINT('Ctrl Pts',(19.2483492267546,21.2646049695469,17.7441794064999));
#191073=CARTESIAN_POINT('Ctrl Pts',(19.2289158894502,21.2693492537257,17.7429918703078));
#191074=CARTESIAN_POINT('Ctrl Pts',(19.2217424611133,21.2710608431452,17.7425528712005));
#191075=CARTESIAN_POINT('Ctrl Pts',(19.2083653142325,21.2741788607841,17.7417329608899));
#191076=CARTESIAN_POINT('Ctrl Pts',(19.2021639001992,21.2755948813547,17.7413523634577));
#191077=CARTESIAN_POINT('Ctrl Pts',(19.1883831752845,21.2786762679187,17.7405054514086));
#191078=CARTESIAN_POINT('Ctrl Pts',(19.1808009267746,21.2803279460318,17.7400387030168));
#191079=CARTESIAN_POINT('Ctrl Pts',(19.158764846024,21.2850014148626,17.7386798823254));
#191080=CARTESIAN_POINT('Ctrl Pts',(19.1442884852242,21.2879136681212,17.737784322947));
#191081=CARTESIAN_POINT('Ctrl Pts',(19.0300817511341,21.3096483698409,17.7306950507874));
#191082=CARTESIAN_POINT('Ctrl Pts',(18.9291597447491,21.3214257443406,17.7242767301331));
#191083=CARTESIAN_POINT('Ctrl Pts',(18.6828357156602,21.3323499372098,17.7082809931213));
#191084=CARTESIAN_POINT('Ctrl Pts',(18.5376112155749,21.3238585078112,17.6985569461534));
#191085=CARTESIAN_POINT('Ctrl Pts',(18.380196148862,21.2982754887016,17.6881851794455));
#191086=CARTESIAN_POINT('Ctrl Pts',(18.3660141538637,21.2958219497368,17.6872526275887));
#191087=CARTESIAN_POINT('Ctrl Pts',(18.337192810706,21.2905324877367,17.6853625878601));
#191088=CARTESIAN_POINT('Ctrl Pts',(18.3225560957591,21.287686121191,17.6844054578225));
#191089=CARTESIAN_POINT('Ctrl Pts',(18.271970368763,21.2772930154982,17.6811095646575));
#191090=CARTESIAN_POINT('Ctrl Pts',(18.2361862742989,21.2689650327601,17.6787991238542));
#191091=CARTESIAN_POINT('Ctrl Pts',(18.1937265790424,21.2579109865741,17.6760973079634));
#191092=CARTESIAN_POINT('Ctrl Pts',(18.1868275058744,21.2560775587583,17.6756595669895));
#191093=CARTESIAN_POINT('Ctrl Pts',(18.1755837192479,21.2530285523958,17.6749483729101));
#191094=CARTESIAN_POINT('Ctrl Pts',(18.1712334496022,21.2518339378875,17.6746737518077));
#191095=CARTESIAN_POINT('Ctrl Pts',(18.1634514332855,21.2496701666862,17.6741835083521));
#191096=CARTESIAN_POINT('Ctrl Pts',(18.1600182987725,21.2487062405505,17.6739675881933));
#191097=CARTESIAN_POINT('Ctrl Pts',(18.1525865592529,21.2465993479337,17.6735009629067));
#191098=CARTESIAN_POINT('Ctrl Pts',(18.148588894267,21.245453276032,17.6732504411495));
#191099=CARTESIAN_POINT('Ctrl Pts',(18.1374263951272,21.2422175251994,17.67255220832));
#191100=CARTESIAN_POINT('Ctrl Pts',(18.1302691144494,21.2401017032923,17.6721059938375));
#191101=CARTESIAN_POINT('Ctrl Pts',(18.0886728884794,21.2275655281857,17.6695205676724));
#191102=CARTESIAN_POINT('Ctrl Pts',(18.0544906744736,21.2163057208929,17.6674273527095));
#191103=CARTESIAN_POINT('Ctrl Pts',(17.9453227525449,21.1772328106099,17.6607946101409));
#191104=CARTESIAN_POINT('Ctrl Pts',(17.8716166476411,21.1460401074211,17.6563959346594));
#191105=CARTESIAN_POINT('Ctrl Pts',(17.6755087981349,21.0496091444333,17.6444820654423));
#191106=CARTESIAN_POINT('Ctrl Pts',(17.5574798616707,20.976413758155,17.6370529466826));
#191107=CARTESIAN_POINT('Ctrl Pts',(17.3992536746686,20.8553309886138,17.6258273988771));
#191108=CARTESIAN_POINT('Ctrl Pts',(17.3526695995275,20.8163963633845,17.6223454084903));
#191109=CARTESIAN_POINT('Ctrl Pts',(17.298710166962,20.7672082799283,17.6180565504279));
#191110=CARTESIAN_POINT('Ctrl Pts',(17.2896683243945,20.7588201176285,17.6173288102015));
#191111=CARTESIAN_POINT('Ctrl Pts',(17.2749135851657,20.744890207889,17.616125942372));
#191112=CARTESIAN_POINT('Ctrl Pts',(17.2691576504602,20.7393943287523,17.6156527858108));
#191113=CARTESIAN_POINT('Ctrl Pts',(17.2588471254062,20.7294378932487,17.6147980768227));
#191114=CARTESIAN_POINT('Ctrl Pts',(17.254281414801,20.7249889518481,17.6144170329893));
#191115=CARTESIAN_POINT('Ctrl Pts',(17.2454688079982,20.7163237866073,17.6136765292058));
#191116=CARTESIAN_POINT('Ctrl Pts',(17.2412195536362,20.7121100392367,17.6133171801826));
#191117=CARTESIAN_POINT('Ctrl Pts',(17.2296415438039,20.7005309977516,17.6123317158141));
#191118=CARTESIAN_POINT('Ctrl Pts',(17.2223491273089,20.6931297483877,17.6117040045766));
#191119=CARTESIAN_POINT('Ctrl Pts',(17.1924047914128,20.6622876319879,17.6090969754829));
#191120=CARTESIAN_POINT('Ctrl Pts',(17.1702422612203,20.6383798116048,17.6070966336874));
#191121=CARTESIAN_POINT('Ctrl Pts',(17.1143839115119,20.5752598173887,17.6018645272729));
#191122=CARTESIAN_POINT('Ctrl Pts',(17.0815581444142,20.5353097642489,17.5985993595146));
#191123=CARTESIAN_POINT('Ctrl Pts',(17.0065533484709,20.4368911293803,17.5906680724658));
#191124=CARTESIAN_POINT('Ctrl Pts',(16.9658348215739,20.3773925694132,17.585960920878));
#191125=CARTESIAN_POINT('Ctrl Pts',(16.8548579529873,20.196026187114,17.5719542995044));
#191126=CARTESIAN_POINT('Ctrl Pts',(16.7936223883586,20.0691226949405,17.5625613341293));
#191127=CARTESIAN_POINT('Ctrl Pts',(16.7454193509487,19.937110186004,17.5536949115506));
#191128=CARTESIAN_POINT('Ctrl Pts',(16.7454194652257,19.9371104989717,17.3329785907215));
#191129=CARTESIAN_POINT('Ctrl Pts',(16.7725602230355,20.0114402087829,17.337312538183));
#191130=CARTESIAN_POINT('Ctrl Pts',(16.8038714332608,20.0842567474831,17.3417076801611));
#191131=CARTESIAN_POINT('Ctrl Pts',(16.8585886909295,20.1940592153942,17.3487130099493));
#191132=CARTESIAN_POINT('Ctrl Pts',(16.8791370174813,20.2323010954823,17.351227264728));
#191133=CARTESIAN_POINT('Ctrl Pts',(16.9067169244504,20.2800478814102,17.354474763141));
#191134=CARTESIAN_POINT('Ctrl Pts',(16.9126730514641,20.2901640047262,17.3551691378256));
#191135=CARTESIAN_POINT('Ctrl Pts',(16.922367974912,20.3063213550115,17.3562886166596));
#191136=CARTESIAN_POINT('Ctrl Pts',(16.9260536348083,20.3123942998627,17.3567117784607));
#191137=CARTESIAN_POINT('Ctrl Pts',(16.9331155510599,20.3238994151,17.3575180641209));
#191138=CARTESIAN_POINT('Ctrl Pts',(16.9364860010985,20.3293350700601,17.3579009712056));
#191139=CARTESIAN_POINT('Ctrl Pts',(16.9442142253304,20.3416734800604,17.3587746784973));
#191140=CARTESIAN_POINT('Ctrl Pts',(16.9485873779769,20.3485664393469,17.3592660448912));
#191141=CARTESIAN_POINT('Ctrl Pts',(16.9600300737485,20.3663738803427,17.3605440298342));
#191142=CARTESIAN_POINT('Ctrl Pts',(16.9671604315237,20.3772486999079,17.3613329088659));
#191143=CARTESIAN_POINT('Ctrl Pts',(17.0144890708334,20.4480013749436,17.3665216444505));
#191144=CARTESIAN_POINT('Ctrl Pts',(17.0576204015997,20.5058512421002,17.3710323454314));
#191145=CARTESIAN_POINT('Ctrl Pts',(17.2306337501685,20.7147388944703,17.3883674657624));
#191146=CARTESIAN_POINT('Ctrl Pts',(17.3786300076174,20.8493823399726,17.4018661683172));
#191147=CARTESIAN_POINT('Ctrl Pts',(17.5665601941078,20.9772301617461,17.4164314443218));
#191148=CARTESIAN_POINT('Ctrl Pts',(17.5901988043808,20.9926294971176,17.4182203772666));
#191149=CARTESIAN_POINT('Ctrl Pts',(17.6242426301299,21.0138503324909,17.4207286344568));
#191150=CARTESIAN_POINT('Ctrl Pts',(17.6343992249504,21.0200629869978,17.4214685155628));
#191151=CARTESIAN_POINT('Ctrl Pts',(17.6501248709692,21.0295007847042,17.4226005253173));
#191152=CARTESIAN_POINT('Ctrl Pts',(17.6556569496467,21.0327866690262,17.4229961934352));
#191153=CARTESIAN_POINT('Ctrl Pts',(17.6648578343665,21.0381951163327,17.4236499206005));
#191154=CARTESIAN_POINT('Ctrl Pts',(17.6685181442491,21.0403319488982,17.4239088543012));
#191155=CARTESIAN_POINT('Ctrl Pts',(17.6756226674773,21.0444509027633,17.4244092059258));
#191156=CARTESIAN_POINT('Ctrl Pts',(17.6790660900925,21.0464343456439,17.4246507070899));
#191157=CARTESIAN_POINT('Ctrl Pts',(17.6855282267345,21.0501324021827,17.4251020046766));
#191158=CARTESIAN_POINT('Ctrl Pts',(17.6885455380733,21.0518492660505,17.425311941548));
#191159=CARTESIAN_POINT('Ctrl Pts',(17.6955600060432,21.0558177213636,17.4257981909739));
#191160=CARTESIAN_POINT('Ctrl Pts',(17.6995602624646,21.0580637445477,17.4260741439447));
#191161=CARTESIAN_POINT('Ctrl Pts',(17.7118939679995,21.0649361120022,17.4269209261227));
#191162=CARTESIAN_POINT('Ctrl Pts',(17.7202515174681,21.0695192680961,17.427489060156));
#191163=CARTESIAN_POINT('Ctrl Pts',(17.8328301191873,21.130270338079,17.4350701511583));
#191164=CARTESIAN_POINT('Ctrl Pts',(17.9415692934468,21.1776640467935,17.4415759625947));
#191165=CARTESIAN_POINT('Ctrl Pts',(18.1572750850971,21.2508620152078,17.4539777147496));
#191166=CARTESIAN_POINT('Ctrl Pts',(18.2634015776809,21.277926440636,17.4598663184589));
#191167=CARTESIAN_POINT('Ctrl Pts',(18.4457333716214,21.3096481423162,17.4701568104535));
#191168=CARTESIAN_POINT('Ctrl Pts',(18.5209629135362,21.3186136102335,17.4744487915918));
#191169=CARTESIAN_POINT('Ctrl Pts',(18.6153647853529,21.3247577549594,17.4799719546709));
#191170=CARTESIAN_POINT('Ctrl Pts',(18.634238700449,21.3257325622059,17.481082862363));
#191171=CARTESIAN_POINT('Ctrl Pts',(18.6616875168986,21.3267819755726,17.4827090989354));
#191172=CARTESIAN_POINT('Ctrl Pts',(18.6702541489368,21.3270574015245,17.4832181384105));
#191173=CARTESIAN_POINT('Ctrl Pts',(18.685271813099,21.3274489577095,17.484113224062));
#191174=CARTESIAN_POINT('Ctrl Pts',(18.6917221828792,21.3275876337977,17.4844985587245));
#191175=CARTESIAN_POINT('Ctrl Pts',(18.7042449731198,21.327799593116,17.4852483935255));
#191176=CARTESIAN_POINT('Ctrl Pts',(18.7103172792509,21.3278762378995,17.4856127843977));
#191177=CARTESIAN_POINT('Ctrl Pts',(18.7248286622531,21.3279969546946,17.4864855297316));
#191178=CARTESIAN_POINT('Ctrl Pts',(18.7332677890517,21.3280166934304,17.4869946421783));
#191179=CARTESIAN_POINT('Ctrl Pts',(18.7636879697191,21.3279059512566,17.4888355887479));
#191180=CARTESIAN_POINT('Ctrl Pts',(18.7856659630545,21.3274835820525,17.4901765150419));
#191181=CARTESIAN_POINT('Ctrl Pts',(18.9943959182488,21.3202192132553,17.5030191343461));
#191182=CARTESIAN_POINT('Ctrl Pts',(19.1794431472078,21.2890192375423,17.5153328733916));
#191183=CARTESIAN_POINT('Ctrl Pts',(19.4337333284128,21.2105880421159,17.5328997662787));
#191184=CARTESIAN_POINT('Ctrl Pts',(19.5081522198843,21.1829708667613,17.5381086118322));
#191185=CARTESIAN_POINT('Ctrl Pts',(19.613663764567,21.1369186202309,17.545445853199));
#191186=CARTESIAN_POINT('Ctrl Pts',(19.6461112997014,21.1217653438801,17.5476949252236));
#191187=CARTESIAN_POINT('Ctrl Pts',(19.6848311993081,21.1024715356176,17.5503563393242));
#191188=CARTESIAN_POINT('Ctrl Pts',(19.6914839790253,21.0991125425504,17.5508128018216));
#191189=CARTESIAN_POINT('Ctrl Pts',(19.7018192539775,21.0938255804594,17.5515204904599));
#191190=CARTESIAN_POINT('Ctrl Pts',(19.7055139677165,21.0919218181571,17.551773191109));
#191191=CARTESIAN_POINT('Ctrl Pts',(19.7123683348977,21.0883644075471,17.5522414270306));
#191192=CARTESIAN_POINT('Ctrl Pts',(19.715529386381,21.0867136725522,17.5524571349789));
#191193=CARTESIAN_POINT('Ctrl Pts',(19.7226827107308,21.0829550950428,17.5529447647721));
#191194=CARTESIAN_POINT('Ctrl Pts',(19.7266724113118,21.080842470649,17.5532163799525));
#191195=CARTESIAN_POINT('Ctrl Pts',(19.738477290575,21.0745431245641,17.55401907963));
#191196=CARTESIAN_POINT('Ctrl Pts',(19.7462730722755,21.0703199933709,17.5545479127832));
#191197=CARTESIAN_POINT('Ctrl Pts',(19.8041311381396,21.0385053590631,17.5584650810947));
#191198=CARTESIAN_POINT('Ctrl Pts',(19.8530887934576,21.0089427107954,17.561736838516));
#191199=CARTESIAN_POINT('Ctrl Pts',(20.0368146583173,20.8875849393916,17.5740815581704));
#191200=CARTESIAN_POINT('Ctrl Pts',(20.1620079583049,20.782325195681,17.582678033751));
#191201=CARTESIAN_POINT('Ctrl Pts',(20.3155037972149,20.6196208636332,17.5950627299056));
#191202=CARTESIAN_POINT('Ctrl Pts',(20.3552033109749,20.5737420894667,17.598468683245));
#191203=CARTESIAN_POINT('Ctrl Pts',(20.4157132092362,20.4974217060215,17.6040604539571));
#191204=CARTESIAN_POINT('Ctrl Pts',(20.4377944175734,20.4680300180912,17.6061972623089));
#191205=CARTESIAN_POINT('Ctrl Pts',(20.4655214805814,20.4290497353363,17.6090172787097));
#191206=CARTESIAN_POINT('Ctrl Pts',(20.4718734630607,20.4199696500724,17.6096732086634));
#191207=CARTESIAN_POINT('Ctrl Pts',(20.4820974114008,20.4051075563819,17.6107454500564));
#191208=CARTESIAN_POINT('Ctrl Pts',(20.486012723312,20.3993555156311,17.611160106472));
#191209=CARTESIAN_POINT('Ctrl Pts',(20.4934941140897,20.3882471569856,17.6119603079193));
#191210=CARTESIAN_POINT('Ctrl Pts',(20.4970642730603,20.3828936700007,17.612345692792));
#191211=CARTESIAN_POINT('Ctrl Pts',(20.5051918090715,20.3705851487282,17.613231205232));
#191212=CARTESIAN_POINT('Ctrl Pts',(20.509732705614,20.3636194067449,17.6137319433897));
#191213=CARTESIAN_POINT('Ctrl Pts',(20.5217064717902,20.3450129289898,17.6150685229631));
#191214=CARTESIAN_POINT('Ctrl Pts',(20.5290665674428,20.3333260473929,17.6159070475437));
#191215=CARTESIAN_POINT('Ctrl Pts',(20.5854499806287,20.2418229028816,17.6224656555343));
#191216=CARTESIAN_POINT('Ctrl Pts',(20.6292349291666,20.1589152438195,17.6283760579522));
#191217=CARTESIAN_POINT('Ctrl Pts',(20.7243942421536,19.9455787281531,17.6434834160732));
#191218=CARTESIAN_POINT('Ctrl Pts',(20.7685887250795,19.8124311045116,17.6528409103574));
#191219=CARTESIAN_POINT('Ctrl Pts',(20.8108330231094,19.6247658258836,17.6654197906971));
#191220=CARTESIAN_POINT('Ctrl Pts',(20.8204433040419,19.5732052543762,17.6688111360771));
#191221=CARTESIAN_POINT('Ctrl Pts',(20.8321596304407,19.4941446232171,17.6738646684591));
#191222=CARTESIAN_POINT('Ctrl Pts',(20.8356596809801,19.4668739241012,17.6755814310299));
#191223=CARTESIAN_POINT('Ctrl Pts',(20.8393686706081,19.4327179916943,17.6776923869868));
#191224=CARTESIAN_POINT('Ctrl Pts',(20.840076441674,19.4258909766083,17.6781123660756));
#191225=CARTESIAN_POINT('Ctrl Pts',(20.8411467367856,19.4150535281288,17.6787758268793));
#191226=CARTESIAN_POINT('Ctrl Pts',(20.8415310355407,19.4110453637206,17.6790205037693));
#191227=CARTESIAN_POINT('Ctrl Pts',(20.8422360871946,19.4034642028226,17.6794819380338));
#191228=CARTESIAN_POINT('Ctrl Pts',(20.8425591900312,19.3998915324176,17.6796988193664));
#191229=CARTESIAN_POINT('Ctrl Pts',(20.8432793871146,19.3916958660629,17.680195052501));
#191230=CARTESIAN_POINT('Ctrl Pts',(20.8436703646585,19.3870723781251,17.6804740582949));
#191231=CARTESIAN_POINT('Ctrl Pts',(20.8446723395946,19.3747408351391,17.6812157964933));
#191232=CARTESIAN_POINT('Ctrl Pts',(20.845256320476,19.3670305726508,17.6816770544119));
#191233=CARTESIAN_POINT('Ctrl Pts',(20.8491566389808,19.3114963005168,17.6849823602183));
#191234=CARTESIAN_POINT('Ctrl Pts',(20.8508902084216,19.2635711109657,17.6877443047049));
#191235=CARTESIAN_POINT('Ctrl Pts',(20.8510570524012,19.1871956969861,17.6920596577943));
#191236=CARTESIAN_POINT('Ctrl Pts',(20.8505464969716,19.1587674833856,17.6936468781337));
#191237=CARTESIAN_POINT('Ctrl Pts',(20.8478034290527,19.0868097947237,17.6976346678849));
#191238=CARTESIAN_POINT('Ctrl Pts',(20.8447990599264,19.0433227144897,17.700017126262));
#191239=CARTESIAN_POINT('Ctrl Pts',(20.8295555435786,18.8911737271371,17.70834212114));
#191240=CARTESIAN_POINT('Ctrl Pts',(20.8102459993496,18.7833979125856,17.7142292058674));
#191241=CARTESIAN_POINT('Ctrl Pts',(20.7636355968937,18.6043751919849,17.7245155785706));
#191242=CARTESIAN_POINT('Ctrl Pts',(20.7406605717448,18.5322320554643,17.7288049202135));
#191243=CARTESIAN_POINT('Ctrl Pts',(20.7071864917377,18.4438096833279,17.7343249019519));
#191244=CARTESIAN_POINT('Ctrl Pts',(20.7002617025218,18.4262320112675,17.7354354298721));
#191245=CARTESIAN_POINT('Ctrl Pts',(20.6898551431418,18.4008190931522,17.7370612112782));
#191246=CARTESIAN_POINT('Ctrl Pts',(20.6865594462201,18.3929082884802,17.7375701803849));
#191247=CARTESIAN_POINT('Ctrl Pts',(20.6806986091872,18.3790774378798,17.7384651846463));
#191248=CARTESIAN_POINT('Ctrl Pts',(20.6781542540807,18.3731486651598,17.7388505086908));
#191249=CARTESIAN_POINT('Ctrl Pts',(20.6731622914622,18.3616617336639,17.7396003542655));
#191250=CARTESIAN_POINT('Ctrl Pts',(20.670717786855,18.3561022890567,17.7399647666774));
#191251=CARTESIAN_POINT('Ctrl Pts',(20.6648188047324,18.3428416127585,17.7408376143543));
#191252=CARTESIAN_POINT('Ctrl Pts',(20.6613421451503,18.3351504156846,17.7413468080064));
#191253=CARTESIAN_POINT('Ctrl Pts',(20.6486422874153,18.3074971154198,17.7431883478214));
#191254=CARTESIAN_POINT('Ctrl Pts',(20.6391544393805,18.2876587542672,17.7445297937903));
#191255=CARTESIAN_POINT('Ctrl Pts',(20.5461505869449,18.10073343788,17.7573680789841));
#191256=CARTESIAN_POINT('Ctrl Pts',(20.4411872885948,17.9452729316278,17.7696761601614));
#191257=CARTESIAN_POINT('Ctrl Pts',(20.2645484207317,17.7462785429009,17.7872413535598));
#191258=CARTESIAN_POINT('Ctrl Pts',(20.2085640850832,17.6899313409217,17.7924537833828));
#191259=CARTESIAN_POINT('Ctrl Pts',(20.1229114919839,17.6129084003772,17.7997953804239));
#191260=CARTESIAN_POINT('Ctrl Pts',(20.0956731975029,17.5896368855449,17.8020453713521));
#191261=CARTESIAN_POINT('Ctrl Pts',(20.062067851755,17.5623701647259,17.8047077227985));
#191262=CARTESIAN_POINT('Ctrl Pts',(20.0562551626246,17.5577045511064,17.805164239308));
#191263=CARTESIAN_POINT('Ctrl Pts',(20.0471626993015,17.5504850191746,17.8058719932761));
#191264=CARTESIAN_POINT('Ctrl Pts',(20.0438999058625,17.5479099502163,17.8061247056742));
#191265=CARTESIAN_POINT('Ctrl Pts',(20.0378236828778,17.5431434350395,17.8065929522284));
#191266=CARTESIAN_POINT('Ctrl Pts',(20.035012327124,17.5409495090687,17.80680865913));
#191267=CARTESIAN_POINT('Ctrl Pts',(20.0286295671,17.5359944292625,17.8072962723943));
#191268=CARTESIAN_POINT('Ctrl Pts',(20.0250548760241,17.5332375954943,17.80756787218));
#191269=CARTESIAN_POINT('Ctrl Pts',(20.0144344205575,17.5251010476585,17.8083704842008));
#191270=CARTESIAN_POINT('Ctrl Pts',(20.0073635530933,17.519754053747,17.8088992458226));
#191271=CARTESIAN_POINT('Ctrl Pts',(19.9544765039958,17.4802805509821,17.8128143882614));
#191272=CARTESIAN_POINT('Ctrl Pts',(19.9073249707374,17.447973497681,17.8160843276193));
#191273=CARTESIAN_POINT('Ctrl Pts',(19.7306678475249,17.3371636798078,17.8277759767483));
#191274=CARTESIAN_POINT('Ctrl Pts',(19.5941509554465,17.270702279564,17.8357918015864));
#191275=CARTESIAN_POINT('Ctrl Pts',(19.3644865293258,17.1879402901132,17.8492377616149));
#191276=CARTESIAN_POINT('Ctrl Pts',(19.2753073678149,17.1622766631443,17.8544436038009));
#191277=CARTESIAN_POINT('Ctrl Pts',(19.1641540250916,17.1380551351852,17.8610701491971));
#191278=CARTESIAN_POINT('Ctrl Pts',(19.1435029882135,17.1338769527762,17.8623066903037));
#191279=CARTESIAN_POINT('Ctrl Pts',(19.113990854512,17.1283631754571,17.8640828166579));
#191280=CARTESIAN_POINT('Ctrl Pts',(19.1051779039577,17.1267744478308,17.864614341065));
#191281=CARTESIAN_POINT('Ctrl Pts',(19.0899348883612,17.1241263046655,17.865535735873));
#191282=CARTESIAN_POINT('Ctrl Pts',(19.0835094765311,17.1230405680707,17.8659247640197));
#191283=CARTESIAN_POINT('Ctrl Pts',(19.0711818098217,17.1210159942013,17.8666723941034));
#191284=CARTESIAN_POINT('Ctrl Pts',(19.0652803833428,17.1200724489254,17.8670308423987));
#191285=CARTESIAN_POINT('Ctrl Pts',(19.0498904953804,17.1176786369862,17.8679670756449));
#191286=CARTESIAN_POINT('Ctrl Pts',(19.0403961045692,17.1162679034589,17.8685461078308));
#191287=CARTESIAN_POINT('Ctrl Pts',(19.0078136638254,17.1116528635474,17.8705383402355));
#191288=CARTESIAN_POINT('Ctrl Pts',(18.9846831061629,17.1087654189029,17.8719614902819));
#191289=CARTESIAN_POINT('Ctrl Pts',(18.7917146785541,17.0879066359558,17.8839119481677));
#191290=CARTESIAN_POINT('Ctrl Pts',(18.6203523441901,17.0901702205066,17.8951011230179));
#191291=CARTESIAN_POINT('Ctrl Pts',(18.3616209376551,17.1250503161618,17.9123532550351));
#191292=CARTESIAN_POINT('Ctrl Pts',(18.2729392378524,17.1428420709198,17.9183162893897));
#191293=CARTESIAN_POINT('Ctrl Pts',(18.1483250946236,17.1762596863198,17.9265592877393));
#191294=CARTESIAN_POINT('Ctrl Pts',(18.1112673324332,17.1872935738502,17.9289921554776));
#191295=CARTESIAN_POINT('Ctrl Pts',(18.0672904398798,17.2017102234611,17.9318402844786));
#191296=CARTESIAN_POINT('Ctrl Pts',(18.0600636236669,17.2041226224891,17.9323070444057));
#191297=CARTESIAN_POINT('Ctrl Pts',(18.0488803793875,17.2079229466031,17.9330271792049));
#191298=CARTESIAN_POINT('Ctrl Pts',(18.0449148714206,17.2092836707796,17.9332821118388));
#191299=CARTESIAN_POINT('Ctrl Pts',(18.037586813933,17.2118225770069,17.9337523971078));
#191300=CARTESIAN_POINT('Ctrl Pts',(18.0342232243212,17.2129974577437,17.9339679355811));
#191301=CARTESIAN_POINT('Ctrl Pts',(18.0266492261547,17.2156644803741,17.9344525589975));
#191302=CARTESIAN_POINT('Ctrl Pts',(18.0224405771749,17.2171614554408,17.9347213533454));
#191303=CARTESIAN_POINT('Ctrl Pts',(18.0101011300934,17.2215945221116,17.9355080658885));
#191304=CARTESIAN_POINT('Ctrl Pts',(18.0019834281366,17.2245671484785,17.9360238640294));
#191305=CARTESIAN_POINT('Ctrl Pts',(17.9455371131738,17.2456302717825,17.9395997093367));
#191306=CARTESIAN_POINT('Ctrl Pts',(17.8978616827471,17.2654343910455,17.9425649576661));
#191307=CARTESIAN_POINT('Ctrl Pts',(17.8310733511714,17.2960872205023,17.9467037793076));
#191308=CARTESIAN_POINT('Ctrl Pts',(17.811334977799,17.3055192761789,17.9479249859216));
#191309=CARTESIAN_POINT('Ctrl Pts',(17.6684463234817,17.3765401560088,17.9567751509095));
#191310=CARTESIAN_POINT('Ctrl Pts',(17.5514174581383,17.4497082187226,17.9640985395546));
#191311=CARTESIAN_POINT('Ctrl Pts',(17.3704328064643,17.5890856997746,17.9766927958227));
#191312=CARTESIAN_POINT('Ctrl Pts',(17.3021869424851,17.6490044419046,17.9817933042145));
#191313=CARTESIAN_POINT('Ctrl Pts',(17.2232621475937,17.7278297618872,17.9882924156419));
#191314=CARTESIAN_POINT('Ctrl Pts',(17.2087435234247,17.7427645117518,17.9895150372841));
#191315=CARTESIAN_POINT('Ctrl Pts',(17.188329651391,17.7643930634187,17.9912746222048));
#191316=CARTESIAN_POINT('Ctrl Pts',(17.1822523881096,17.7709139606174,17.9918037316272));
#191317=CARTESIAN_POINT('Ctrl Pts',(17.1718088759356,17.7822627039517,17.9927222751508));
#191318=CARTESIAN_POINT('Ctrl Pts',(17.1674233461454,17.7870727001132,17.9931108812248));
#191319=CARTESIAN_POINT('Ctrl Pts',(17.1590478682053,17.7963443500479,17.9938586422213));
#191320=CARTESIAN_POINT('Ctrl Pts',(17.1550545168643,17.8008028557936,17.9942176480252));
#191321=CARTESIAN_POINT('Ctrl Pts',(17.1446737496373,17.8124921690202,17.9951574342582));
#191322=CARTESIAN_POINT('Ctrl Pts',(17.1383168156392,17.819749751579,17.9957394805563));
#191323=CARTESIAN_POINT('Ctrl Pts',(17.1165781267832,17.8449133613392,17.9977528026145));
#191324=CARTESIAN_POINT('Ctrl Pts',(17.1014468237556,17.8630325388784,17.999194313112));
#191325=CARTESIAN_POINT('Ctrl Pts',(16.9829318799082,18.0098729067035,18.010816152123));
#191326=CARTESIAN_POINT('Ctrl Pts',(16.8946445826061,18.150010919624,18.021610011477));
#191327=CARTESIAN_POINT('Ctrl Pts',(16.7685612817754,18.4141145820774,18.040949937191));
#191328=CARTESIAN_POINT('Ctrl Pts',(16.7241006265763,18.5340310221172,18.0493910395935));
#191329=CARTESIAN_POINT('Ctrl Pts',(16.6875909745639,18.6687441998302,18.0580465200214));
#191330=CARTESIAN_POINT('Ctrl Pts',(16.684568363399,18.6802823404743,18.0587812938641));
#191331=CARTESIAN_POINT('Ctrl Pts',(16.6804108697503,18.6967180319683,18.0598180380657));
#191332=CARTESIAN_POINT('Ctrl Pts',(16.6791957303689,18.7015947848483,18.0601244218867));
#191333=CARTESIAN_POINT('Ctrl Pts',(16.6771318955092,18.7100051828676,18.060650624776));
#191334=CARTESIAN_POINT('Ctrl Pts',(16.6762749145256,18.7135367556761,18.0608709177079));
#191335=CARTESIAN_POINT('Ctrl Pts',(16.6746311948272,18.7203873639313,18.0612969424028));
#191336=CARTESIAN_POINT('Ctrl Pts',(16.673843383718,18.7237060936567,18.0615027380218));
#191337=CARTESIAN_POINT('Ctrl Pts',(16.6717400399649,18.7326629061109,18.0620566006581));
#191338=CARTESIAN_POINT('Ctrl Pts',(16.6704395975616,18.7383045531905,18.0624038061267));
#191339=CARTESIAN_POINT('Ctrl Pts',(16.6657019231811,18.7592499785667,18.0636869544939));
#191340=CARTESIAN_POINT('Ctrl Pts',(16.6624115604281,18.7745869090283,18.064614851161));
#191341=CARTESIAN_POINT('Ctrl Pts',(16.6325545374803,18.9217095916557,18.0734167669213));
#191342=CARTESIAN_POINT('Ctrl Pts',(16.6184239749364,19.055726048318,18.0806878996701));
#191343=CARTESIAN_POINT('Ctrl Pts',(16.6170404620324,19.1964794404447,18.088331826678));
#191344=CARTESIAN_POINT('Ctrl Pts',(16.6170066729089,19.2027668310727,18.0886732592247));
#191345=CARTESIAN_POINT('Ctrl Pts',(16.6168668547703,19.3548927710488,18.0969354872158));
#191346=CARTESIAN_POINT('Ctrl Pts',(16.6318021056912,19.5003359780539,18.1048962031172));
#191347=CARTESIAN_POINT('Ctrl Pts',(16.6664676958081,19.6666057136677,18.1147554617558));
#191348=CARTESIAN_POINT('Ctrl Pts',(16.6717720454849,19.6900429933476,18.1161622442136));
#191349=CARTESIAN_POINT('Ctrl Pts',(16.679780444527,19.7228256319992,18.1181559734912));
#191350=CARTESIAN_POINT('Ctrl Pts',(16.6821518243893,19.7322509176174,18.118732225555));
#191351=CARTESIAN_POINT('Ctrl Pts',(16.68609161862,19.7474664424257,18.1196675334439));
#191352=CARTESIAN_POINT('Ctrl Pts',(16.6876199074602,19.7532669988962,18.1200252880178));
#191353=CARTESIAN_POINT('Ctrl Pts',(16.6908553251685,19.7653384122078,18.1207723208982));
#191354=CARTESIAN_POINT('Ctrl Pts',(16.6925667172331,19.7716080521106,18.1211617342632));
#191355=CARTESIAN_POINT('Ctrl Pts',(16.6966783608732,19.7864024424684,18.1220840319993));
#191356=CARTESIAN_POINT('Ctrl Pts',(16.699103276067,19.7949201582881,18.1226177143265));
#191357=CARTESIAN_POINT('Ctrl Pts',(16.7073169333128,19.823098686354,18.1243922887777));
#191358=CARTESIAN_POINT('Ctrl Pts',(16.7133375993579,19.8426901700239,18.1256407216567));
#191359=CARTESIAN_POINT('Ctrl Pts',(16.7277680314605,19.8873285000079,18.128519727433));
#191360=CARTESIAN_POINT('Ctrl Pts',(16.7363623469838,19.9123059881422,18.1301558675295));
#191361=CARTESIAN_POINT('Ctrl Pts',(16.7454193782244,19.9371102607032,18.1318062886951));
#191362=CARTESIAN_POINT('Origin',(18.734,19.211,0.));
#191363=CARTESIAN_POINT('',(16.7477767826476,19.936270776259,19.1554367658253));
#191364=CARTESIAN_POINT('',(16.7454193714968,19.9371102422787,18.9348454715054));
#191365=CARTESIAN_POINT('',(16.7454193623258,19.9371102171621,0.));
#191366=CARTESIAN_POINT('',(16.6180378694014,19.2091158125652,19.1109437209775));
#191367=CARTESIAN_POINT('Ctrl Pts',(16.6180378694014,19.2091158125652,19.1109437209775));
#191368=CARTESIAN_POINT('Ctrl Pts',(16.6201500192997,19.4559462490499,19.1257747359268));
#191369=CARTESIAN_POINT('Ctrl Pts',(16.6645218722682,19.7034418982865,19.1406057508761));
#191370=CARTESIAN_POINT('Ctrl Pts',(16.7477767826476,19.936270776259,19.1554367658253));
#191371=CARTESIAN_POINT('Ctrl Pts',(16.6170008744685,19.2090758122038,19.1115401841555));
#191372=CARTESIAN_POINT('Ctrl Pts',(16.6171446318861,19.0509133251653,19.1011782561604));
#191373=CARTESIAN_POINT('Ctrl Pts',(16.6350118723612,18.8932596446619,19.0905432530762));
#191374=CARTESIAN_POINT('Ctrl Pts',(16.6745229994948,18.7204833194059,19.079322975751));
#191375=CARTESIAN_POINT('Ctrl Pts',(16.6790219066614,18.7019644230679,19.0781267294454));
#191376=CARTESIAN_POINT('Ctrl Pts',(16.6870567960829,18.6707348074463,19.0761231159487));
#191377=CARTESIAN_POINT('Ctrl Pts',(16.6904625692902,18.6579920906677,19.0753094665024));
#191378=CARTESIAN_POINT('Ctrl Pts',(16.6953858358077,18.6402385095914,19.0741821138998));
#191379=CARTESIAN_POINT('Ctrl Pts',(16.696803075031,18.6352004866086,19.0738629058709));
#191380=CARTESIAN_POINT('Ctrl Pts',(16.6992465311558,18.6266364092212,19.0733215531984));
#191381=CARTESIAN_POINT('Ctrl Pts',(16.7002632616391,18.6231076927154,19.0730988626086));
#191382=CARTESIAN_POINT('Ctrl Pts',(16.7022279707194,18.6163549685451,19.0726734366951));
#191383=CARTESIAN_POINT('Ctrl Pts',(16.7031744467514,18.6131305618798,19.0724706126738));
#191384=CARTESIAN_POINT('Ctrl Pts',(16.7056983609903,18.6046073662642,19.071935282468));
#191385=CARTESIAN_POINT('Ctrl Pts',(16.7072888975922,18.5993124375942,19.0716035366446));
#191386=CARTESIAN_POINT('Ctrl Pts',(16.712985869796,18.5806132784766,19.0704346777269));
#191387=CARTESIAN_POINT('Ctrl Pts',(16.7172047908137,18.5672433372347,19.0696038727208));
#191388=CARTESIAN_POINT('Ctrl Pts',(16.7728160464388,18.3969234067356,19.0590717551862));
#191389=CARTESIAN_POINT('Ctrl Pts',(16.8422782435161,18.24644367624,19.0502965055289));
#191390=CARTESIAN_POINT('Ctrl Pts',(16.977247552425,18.0260063150719,19.0362193600941));
#191391=CARTESIAN_POINT('Ctrl Pts',(17.0311543347221,17.9497689381889,19.0310910973721));
#191392=CARTESIAN_POINT('Ctrl Pts',(17.1208715353498,17.8391686547966,19.0229954307018));
#191393=CARTESIAN_POINT('Ctrl Pts',(17.1531525290882,17.8020907039695,19.0201570650561));
#191394=CARTESIAN_POINT('Ctrl Pts',(17.1948767039491,17.7574071160473,19.0165592066886));
#191395=CARTESIAN_POINT('Ctrl Pts',(17.203134859877,17.7487125089201,19.0158504009069));
#191396=CARTESIAN_POINT('Ctrl Pts',(17.2157051973563,17.735701009314,19.0147761657928));
#191397=CARTESIAN_POINT('Ctrl Pts',(17.2199629962938,17.7313317365476,19.0144131009373));
#191398=CARTESIAN_POINT('Ctrl Pts',(17.2286998576546,17.7224433280528,19.0136696899763));
#191399=CARTESIAN_POINT('Ctrl Pts',(17.2331805232222,17.7179258622221,19.0132892752671));
#191400=CARTESIAN_POINT('Ctrl Pts',(17.2428809663014,17.7082335337445,19.0124674578117));
#191401=CARTESIAN_POINT('Ctrl Pts',(17.2481074531288,17.7030655313342,19.0120257590825));
#191402=CARTESIAN_POINT('Ctrl Pts',(17.2623110340044,17.6891664326575,19.0108282464363));
#191403=CARTESIAN_POINT('Ctrl Pts',(17.2713387540473,17.6804877039545,19.0100701614586));
#191404=CARTESIAN_POINT('Ctrl Pts',(17.3151231024102,17.6391371547627,19.0064074842921));
#191405=CARTESIAN_POINT('Ctrl Pts',(17.3508980821952,17.6075683786899,19.0034563260724));
#191406=CARTESIAN_POINT('Ctrl Pts',(17.4044074251072,17.5634743082188,18.9990976615589));
#191407=CARTESIAN_POINT('Ctrl Pts',(17.4213179024832,17.5499693014145,18.9977279099325));
#191408=CARTESIAN_POINT('Ctrl Pts',(17.5359996072933,17.4612275727666,18.988491042975));
#191409=CARTESIAN_POINT('Ctrl Pts',(17.6399710417779,17.3944088906082,18.9803477036228));
#191410=CARTESIAN_POINT('Ctrl Pts',(17.8256695346015,17.2968170893918,18.9664878059363));
#191411=CARTESIAN_POINT('Ctrl Pts',(17.9045801611799,17.2613269292849,18.9607924778697));
#191412=CARTESIAN_POINT('Ctrl Pts',(18.0206872900517,17.2174369719483,18.9528685869228));
#191413=CARTESIAN_POINT('Ctrl Pts',(18.0562824698198,17.2050568492692,18.9504988218728));
#191414=CARTESIAN_POINT('Ctrl Pts',(18.0993990009962,17.191339687713,18.9477146269606));
#191415=CARTESIAN_POINT('Ctrl Pts',(18.1066188021647,17.189085303102,18.947251291168));
#191416=CARTESIAN_POINT('Ctrl Pts',(18.117847702612,17.1856450132175,18.9465352929473));
#191417=CARTESIAN_POINT('Ctrl Pts',(18.1218484095555,17.1844322347686,18.9462811006578));
#191418=CARTESIAN_POINT('Ctrl Pts',(18.1292663852579,17.1822075127206,18.9458115015063));
#191419=CARTESIAN_POINT('Ctrl Pts',(18.1326825870252,17.1811923563079,18.9455959131568));
#191420=CARTESIAN_POINT('Ctrl Pts',(18.1404012307193,17.1789198854211,18.9451103214075));
#191421=CARTESIAN_POINT('Ctrl Pts',(18.1447050996938,17.1776676090021,18.9448406138121));
#191422=CARTESIAN_POINT('Ctrl Pts',(18.1573895663868,17.1740205263338,18.9440487418058));
#191423=CARTESIAN_POINT('Ctrl Pts',(18.1657811310127,17.171663762121,18.9435287393929));
#191424=CARTESIAN_POINT('Ctrl Pts',(18.2255697927548,17.155269862724,18.9398497134708));
#191425=CARTESIAN_POINT('Ctrl Pts',(18.2774706936795,17.1431243553732,18.9367918179557));
#191426=CARTESIAN_POINT('Ctrl Pts',(18.3462353565157,17.1297482997449,18.9328519248876));
#191427=CARTESIAN_POINT('Ctrl Pts',(18.3627294652925,17.1267427535456,18.9319152393935));
#191428=CARTESIAN_POINT('Ctrl Pts',(18.5244232211533,17.0992593978775,18.922799715624));
#191429=CARTESIAN_POINT('Ctrl Pts',(18.6717693275649,17.0897971408996,18.9149907051229));
#191430=CARTESIAN_POINT('Ctrl Pts',(18.8815354652985,17.0982173395463,18.9033840281849));
#191431=CARTESIAN_POINT('Ctrl Pts',(18.9440143547471,17.1035108859474,18.8998691598699));
#191432=CARTESIAN_POINT('Ctrl Pts',(19.0308678364961,17.1147702745931,18.8948446728013));
#191433=CARTESIAN_POINT('Ctrl Pts',(19.0555132099377,17.118408602556,18.8934033807674));
#191434=CARTESIAN_POINT('Ctrl Pts',(19.0985484524535,17.1255399609929,18.8908560572443));
#191435=CARTESIAN_POINT('Ctrl Pts',(19.1169671350349,17.1288435964872,18.8897559561322));
#191436=CARTESIAN_POINT('Ctrl Pts',(19.1437211571363,17.1340092801898,18.8881426764918));
#191437=CARTESIAN_POINT('Ctrl Pts',(19.1520931746421,17.1356783452091,18.8876356451222));
#191438=CARTESIAN_POINT('Ctrl Pts',(19.1667692138209,17.138696603749,18.8867428793555));
#191439=CARTESIAN_POINT('Ctrl Pts',(19.1730776325759,17.1400240489814,18.8863578449666));
#191440=CARTESIAN_POINT('Ctrl Pts',(19.1853266308028,17.1426600196209,18.8856076916917));
#191441=CARTESIAN_POINT('Ctrl Pts',(19.191267832834,17.1439653776579,18.8852426778275));
#191442=CARTESIAN_POINT('Ctrl Pts',(19.2054753784591,17.1471512081117,18.8843669771951));
#191443=CARTESIAN_POINT('Ctrl Pts',(19.2137361658393,17.1490557533757,18.8838555208074));
#191444=CARTESIAN_POINT('Ctrl Pts',(19.2436129849782,17.1561331879254,18.8819972936995));
#191445=CARTESIAN_POINT('Ctrl Pts',(19.2651580661746,17.1615966576936,18.8806412066991));
#191446=CARTESIAN_POINT('Ctrl Pts',(19.4646170644369,17.2155325742307,18.8679328061335));
#191447=CARTESIAN_POINT('Ctrl Pts',(19.6355380335178,17.2867095772915,18.8557929015899));
#191448=CARTESIAN_POINT('Ctrl Pts',(19.8650839116962,17.4196624368959,18.8382772653005));
#191449=CARTESIAN_POINT('Ctrl Pts',(19.9327485112884,17.4642187231329,18.832956966012));
#191450=CARTESIAN_POINT('Ctrl Pts',(20.0267770771401,17.534178586528,18.8254845213215));
#191451=CARTESIAN_POINT('Ctrl Pts',(20.0552970612864,17.5565583830546,18.8232070864157));
#191452=CARTESIAN_POINT('Ctrl Pts',(20.0889935523643,17.5844277109654,18.8205167584507));
#191453=CARTESIAN_POINT('Ctrl Pts',(20.0947317457668,17.589225028463,18.8200586409381));
#191454=CARTESIAN_POINT('Ctrl Pts',(20.1036234852616,17.5967392305256,18.8193489506928));
#191455=CARTESIAN_POINT('Ctrl Pts',(20.1067945806816,17.599435119772,18.819095890203));
#191456=CARTESIAN_POINT('Ctrl Pts',(20.1126674640503,17.6044578322296,18.818627327821));
#191457=CARTESIAN_POINT('Ctrl Pts',(20.1153712989724,17.6067821070972,18.8184116511215));
#191458=CARTESIAN_POINT('Ctrl Pts',(20.1214793240839,17.6120595901345,18.8179245239223));
#191459=CARTESIAN_POINT('Ctrl Pts',(20.1248799553518,17.6150168360146,18.817653377421));
#191460=CARTESIAN_POINT('Ctrl Pts',(20.1349148347956,17.6237997680625,18.816853344491));
#191461=CARTESIAN_POINT('Ctrl Pts',(20.1415222057417,17.629656205282,18.8163266872344));
#191462=CARTESIAN_POINT('Ctrl Pts',(20.1898927829367,17.6730727902719,18.8124703669765));
#191463=CARTESIAN_POINT('Ctrl Pts',(20.2301869412565,17.712243946896,18.8092532249539));
#191464=CARTESIAN_POINT('Ctrl Pts',(20.3730796475201,17.862668644287,18.7976120775301));
#191465=CARTESIAN_POINT('Ctrl Pts',(20.465226287986,17.9832211992772,18.7896009979635));
#191466=CARTESIAN_POINT('Ctrl Pts',(20.5973880215622,18.2009674269824,18.7755780329373));
#191467=CARTESIAN_POINT('Ctrl Pts',(20.6444839278699,18.2931613175155,18.7697622949186));
#191468=CARTESIAN_POINT('Ctrl Pts',(20.6904114891585,18.4020731394506,18.7628289767306));
#191469=CARTESIAN_POINT('Ctrl Pts',(20.6960256337505,18.4157868358518,18.7619550699364));
#191470=CARTESIAN_POINT('Ctrl Pts',(20.7043637100952,18.4367802394936,18.7606154479331));
#191471=CARTESIAN_POINT('Ctrl Pts',(20.7071923592345,18.444018058483,18.7601532661381));
#191472=CARTESIAN_POINT('Ctrl Pts',(20.7122640596845,18.4572090606539,18.7593102765595));
#191473=CARTESIAN_POINT('Ctrl Pts',(20.7145202575037,18.4631571165473,18.7589299156492));
#191474=CARTESIAN_POINT('Ctrl Pts',(20.71933097412,18.4760141617821,18.7581071835731));
#191475=CARTESIAN_POINT('Ctrl Pts',(20.7218763051152,18.4829264785713,18.7576645109143));
#191476=CARTESIAN_POINT('Ctrl Pts',(20.7286748283063,18.5016905595348,18.7564618263254));
#191477=CARTESIAN_POINT('Ctrl Pts',(20.7328583885205,18.5135670749731,18.755699510201));
#191478=CARTESIAN_POINT('Ctrl Pts',(20.7526313999011,18.5713393798464,18.7519855029524));
#191479=CARTESIAN_POINT('Ctrl Pts',(20.7667463907695,18.6177210225686,18.7489856587955));
#191480=CARTESIAN_POINT('Ctrl Pts',(20.7897993786112,18.7040028423859,18.7433682729105));
#191481=CARTESIAN_POINT('Ctrl Pts',(20.7991975642982,18.7437571254747,18.7407660864017));
#191482=CARTESIAN_POINT('Ctrl Pts',(20.8345936369177,18.9155365054141,18.7294716584824));
#191483=CARTESIAN_POINT('Ctrl Pts',(20.8491209798667,19.049598811803,18.7205051558096));
#191484=CARTESIAN_POINT('Ctrl Pts',(20.8516254590161,19.2468084022229,18.7075444977657));
#191485=CARTESIAN_POINT('Ctrl Pts',(20.8496363024119,19.3095086864417,18.7034626440817));
#191486=CARTESIAN_POINT('Ctrl Pts',(20.8425144307473,19.4028647468615,18.6975223401024));
#191487=CARTESIAN_POINT('Ctrl Pts',(20.839486884562,19.4336441061345,18.6955864335863));
#191488=CARTESIAN_POINT('Ctrl Pts',(20.8349328272353,19.4714247792975,18.6932469393481));
#191489=CARTESIAN_POINT('Ctrl Pts',(20.8340440306902,19.4784974443281,18.6928105715904));
#191490=CARTESIAN_POINT('Ctrl Pts',(20.8325896919388,19.489616211027,18.6921272202171));
#191491=CARTESIAN_POINT('Ctrl Pts',(20.8320481419577,19.4936653194835,18.6918789189539));
#191492=CARTESIAN_POINT('Ctrl Pts',(20.8310106013006,19.5012556176519,18.6914145351768));
#191493=CARTESIAN_POINT('Ctrl Pts',(20.8305173653483,19.5047970771597,18.69119830639));
#191494=CARTESIAN_POINT('Ctrl Pts',(20.8293663494303,19.5129109141838,18.6907038996592));
#191495=CARTESIAN_POINT('Ctrl Pts',(20.8287025761784,19.5174823921645,18.6904260636672));
#191496=CARTESIAN_POINT('Ctrl Pts',(20.8265994626474,19.5316407128541,18.6895677129786));
#191497=CARTESIAN_POINT('Ctrl Pts',(20.8251092083838,19.5412200243705,18.688990001313));
#191498=CARTESIAN_POINT('Ctrl Pts',(20.8075258664512,19.6493498686095,18.6824997969179));
#191499=CARTESIAN_POINT('Ctrl Pts',(20.7845428933871,19.7466671043616,18.6769464824106));
#191500=CARTESIAN_POINT('Ctrl Pts',(20.7039194330605,20.0048593052985,18.6621439395176));
#191501=CARTESIAN_POINT('Ctrl Pts',(20.633573517495,20.1609545822545,18.653067698507));
#191502=CARTESIAN_POINT('Ctrl Pts',(20.5300529974278,20.3320465585058,18.6416591573074));
#191503=CARTESIAN_POINT('Ctrl Pts',(20.5143266916917,20.3568571070566,18.6399671516229));
#191504=CARTESIAN_POINT('Ctrl Pts',(20.4863141012396,20.3990816559,18.6370162701542));
#191505=CARTESIAN_POINT('Ctrl Pts',(20.4742714985293,20.4166524346378,18.6357663111838));
#191506=CARTESIAN_POINT('Ctrl Pts',(20.4567698132821,20.441379645134,18.6339742543207));
#191507=CARTESIAN_POINT('Ctrl Pts',(20.4515268272503,20.448687963337,18.6334404193319));
#191508=CARTESIAN_POINT('Ctrl Pts',(20.4424010758871,20.4612389058725,18.6325162915029));
#191509=CARTESIAN_POINT('Ctrl Pts',(20.4385403287738,20.4664974408433,18.6321268545737));
#191510=CARTESIAN_POINT('Ctrl Pts',(20.4311012300654,20.4765323118091,18.6313793287589));
#191511=CARTESIAN_POINT('Ctrl Pts',(20.4275268604804,20.4813115322708,18.6310213977949));
#191512=CARTESIAN_POINT('Ctrl Pts',(20.4181787953514,20.4937010709986,18.6300884772442));
#191513=CARTESIAN_POINT('Ctrl Pts',(20.412373760527,20.5012874747701,18.6295122577315));
#191514=CARTESIAN_POINT('Ctrl Pts',(20.3923987975938,20.527029189114,18.6275398506332));
#191515=CARTESIAN_POINT('Ctrl Pts',(20.3779844348143,20.5449919455557,18.6261339782034));
#191516=CARTESIAN_POINT('Ctrl Pts',(20.2515399471054,20.6974008857603,18.6139442887581));
#191517=CARTESIAN_POINT('Ctrl Pts',(20.1235499347325,20.8176869054586,18.6024611893005));
#191518=CARTESIAN_POINT('Ctrl Pts',(19.9117078059211,20.9723414260378,18.5851311314825));
#191519=CARTESIAN_POINT('Ctrl Pts',(19.8380318327756,21.0194343873001,18.579373310981));
#191520=CARTESIAN_POINT('Ctrl Pts',(19.7285100650725,21.0802447153362,18.5713747003021));
#191521=CARTESIAN_POINT('Ctrl Pts',(19.694876561165,21.0977545474171,18.5689900008643));
#191522=CARTESIAN_POINT('Ctrl Pts',(19.6539766352162,21.1176697134146,18.5661906590325));
#191523=CARTESIAN_POINT('Ctrl Pts',(19.6471467563052,21.1209501068958,18.5657265026955));
#191524=CARTESIAN_POINT('Ctrl Pts',(19.6365187160276,21.1259847172551,18.5650095130134));
#191525=CARTESIAN_POINT('Ctrl Pts',(19.6327327985033,21.1277644241518,18.5647551431406));
#191526=CARTESIAN_POINT('Ctrl Pts',(19.6257120429482,21.1310394089649,18.5642853799682));
#191527=CARTESIAN_POINT('Ctrl Pts',(19.622478732703,21.1325377283185,18.5640698041362));
#191528=CARTESIAN_POINT('Ctrl Pts',(19.6151733639526,21.1359006624295,18.563584447185));
#191529=CARTESIAN_POINT('Ctrl Pts',(19.6110991744573,21.1377605187399,18.56331496061));
#191530=CARTESIAN_POINT('Ctrl Pts',(19.5990944870889,21.1431946577611,18.5625243387259));
#191531=CARTESIAN_POINT('Ctrl Pts',(19.5911477153395,21.1467330567638,18.5620053552151));
#191532=CARTESIAN_POINT('Ctrl Pts',(19.5346679266463,21.1714653726992,18.5583462580914));
#191533=CARTESIAN_POINT('Ctrl Pts',(19.4853721754551,21.1908824359157,18.5553060530459));
#191534=CARTESIAN_POINT('Ctrl Pts',(19.432975422838,21.2092814964535,18.5521819430909));
#191535=CARTESIAN_POINT('Ctrl Pts',(19.4305534542855,21.2101270260325,18.5520377726349));
#191536=CARTESIAN_POINT('Ctrl Pts',(19.28888825286,21.2592948382756,18.5436185346475));
#191537=CARTESIAN_POINT('Ctrl Pts',(19.1449736961195,21.2929507341865,18.5358030041243));
#191538=CARTESIAN_POINT('Ctrl Pts',(18.9017575108409,21.3236045397095,18.522332865265));
#191539=CARTESIAN_POINT('Ctrl Pts',(18.8040736013577,21.3290951267861,18.5168602208469));
#191540=CARTESIAN_POINT('Ctrl Pts',(18.6847002070269,21.3275368045576,18.5099105016166));
#191541=CARTESIAN_POINT('Ctrl Pts',(18.6630400081951,21.3269213461122,18.50863931014));
#191542=CARTESIAN_POINT('Ctrl Pts',(18.6323459828862,21.3255773757285,18.5068220743304));
#191543=CARTESIAN_POINT('Ctrl Pts',(18.6233010650617,21.3251231655373,18.5062846177478));
#191544=CARTESIAN_POINT('Ctrl Pts',(18.6077349656487,21.3242413129037,18.5053561970239));
#191545=CARTESIAN_POINT('Ctrl Pts',(18.6012122893559,21.3238414819593,18.5049661102912));
#191546=CARTESIAN_POINT('Ctrl Pts',(18.5887491436962,21.3230195679499,18.5042187088812));
#191547=CARTESIAN_POINT('Ctrl Pts',(18.5828083906047,21.3226026053172,18.5038615587449));
#191548=CARTESIAN_POINT('Ctrl Pts',(18.5674130575754,21.3214567540521,18.5029336683251));
#191549=CARTESIAN_POINT('Ctrl Pts',(18.5579615510795,21.3206894036886,18.502361724281));
#191550=CARTESIAN_POINT('Ctrl Pts',(18.5259969567312,21.3178779622611,18.5004194999191));
#191551=CARTESIAN_POINT('Ctrl Pts',(18.5035121648374,21.3155368396718,18.4990399320636));
#191552=CARTESIAN_POINT('Ctrl Pts',(18.3020367776365,21.2912917518554,18.4865540263959));
#191553=CARTESIAN_POINT('Ctrl Pts',(18.126522023175,21.2469644250179,18.4746992431691));
#191554=CARTESIAN_POINT('Ctrl Pts',(17.8809239452282,21.1503173711543,18.457266167439));
#191555=CARTESIAN_POINT('Ctrl Pts',(17.8049400283445,21.1150850862071,18.4517595274105));
#191556=CARTESIAN_POINT('Ctrl Pts',(17.6986815510754,21.0579356125403,18.4440621110421));
#191557=CARTESIAN_POINT('Ctrl Pts',(17.6665878142559,21.0395751442088,18.441738211702));
#191558=CARTESIAN_POINT('Ctrl Pts',(17.628560205465,21.0164773447493,18.4390005974839));
#191559=CARTESIAN_POINT('Ctrl Pts',(17.6221518897594,21.0125380554962,18.4385398221759));
#191560=CARTESIAN_POINT('Ctrl Pts',(17.612222573122,21.0063611908496,18.4378269185483));
#191561=CARTESIAN_POINT('Ctrl Pts',(17.6086870339041,21.0041472694934,18.4375732810896));
#191562=CARTESIAN_POINT('Ctrl Pts',(17.6021424115697,21.0000221089793,18.4371041920685));
#191563=CARTESIAN_POINT('Ctrl Pts',(17.5991316390303,20.9981137374163,18.4368885622889));
#191564=CARTESIAN_POINT('Ctrl Pts',(17.5923359204867,20.9937821869968,18.4364022263877));
#191565=CARTESIAN_POINT('Ctrl Pts',(17.5885538720852,20.9913545617728,18.4361318200516));
#191566=CARTESIAN_POINT('Ctrl Pts',(17.5774136148093,20.9841536481285,18.4353359899103));
#191567=CARTESIAN_POINT('Ctrl Pts',(17.5700772025157,20.9793465875771,18.4348127605566));
#191568=CARTESIAN_POINT('Ctrl Pts',(17.5172409369551,20.9442552397793,18.43104915654));
#191569=CARTESIAN_POINT('Ctrl Pts',(17.4728950096634,20.9122617776047,18.4279152663074));
#191570=CARTESIAN_POINT('Ctrl Pts',(17.2972524478794,20.7748971618022,18.4153889431912));
#191571=CARTESIAN_POINT('Ctrl Pts',(17.1775040230281,20.6557649172382,18.4065304719811));
#191572=CARTESIAN_POINT('Ctrl Pts',(17.0365796713678,20.4774622475054,18.3939311490437));
#191573=CARTESIAN_POINT('Ctrl Pts',(17.0019842701858,20.4297219305364,18.3906172155171));
#191574=CARTESIAN_POINT('Ctrl Pts',(16.9495311525094,20.3505862367684,18.3851630442936));
#191575=CARTESIAN_POINT('Ctrl Pts',(16.9304053321228,20.3200680350769,18.3830687233733));
#191576=CARTESIAN_POINT('Ctrl Pts',(16.9064660612584,20.2796111120302,18.3802971022042));
#191577=CARTESIAN_POINT('Ctrl Pts',(16.900938149018,20.2701006796203,18.3796459090695));
#191578=CARTESIAN_POINT('Ctrl Pts',(16.8920438950786,20.2545204238581,18.3785794813268));
#191579=CARTESIAN_POINT('Ctrl Pts',(16.8886327968082,20.2484762894096,18.3781658675899));
#191580=CARTESIAN_POINT('Ctrl Pts',(16.8821134589856,20.2367907801168,18.3773663281304));
#191581=CARTESIAN_POINT('Ctrl Pts',(16.8790011194907,20.2311517716744,18.3769805552877));
#191582=CARTESIAN_POINT('Ctrl Pts',(16.8719106759571,20.218165407329,18.3760922253791));
#191583=CARTESIAN_POINT('Ctrl Pts',(16.8679502574876,20.2108085635652,18.3755890447085));
#191584=CARTESIAN_POINT('Ctrl Pts',(16.8574949080592,20.19110825083,18.3742416889693));
#191585=CARTESIAN_POINT('Ctrl Pts',(16.8510783244572,20.1787238720736,18.3733947618489));
#191586=CARTESIAN_POINT('Ctrl Pts',(16.8071710292921,20.0918900903104,18.3674560690453));
#191587=CARTESIAN_POINT('Ctrl Pts',(16.773994207962,20.0153674650894,18.3622160460457));
#191588=CARTESIAN_POINT('Ctrl Pts',(16.7454193519082,19.9371101886317,18.3568545479166));
#191589=CARTESIAN_POINT('',(16.6170000449378,19.2114361958265,18.8870727828678));
#191590=CARTESIAN_POINT('Ctrl Pts',(16.7454193782244,19.9371102607032,18.1318062886951));
#191591=CARTESIAN_POINT('Ctrl Pts',(16.7665449537571,19.9949663638349,18.1356559052053));
#191592=CARTESIAN_POINT('Ctrl Pts',(16.7901879214744,20.0518800190739,18.139584314016));
#191593=CARTESIAN_POINT('Ctrl Pts',(16.8711047761691,20.2249340166287,18.15195208795));
#191594=CARTESIAN_POINT('Ctrl Pts',(16.9365617184093,20.336900875137,18.1605860036748));
#191595=CARTESIAN_POINT('Ctrl Pts',(17.0275714615357,20.4642053831557,18.1708506020951));
#191596=CARTESIAN_POINT('Ctrl Pts',(17.0437392986115,20.4859278119496,18.1726183621046));
#191597=CARTESIAN_POINT('Ctrl Pts',(17.095497683323,20.5527523667523,18.1780952033794));
#191598=CARTESIAN_POINT('Ctrl Pts',(17.1325132652244,20.5967239096791,18.1817560584367));
#191599=CARTESIAN_POINT('Ctrl Pts',(17.1772633068432,20.6456911367769,18.185849319262));
#191600=CARTESIAN_POINT('Ctrl Pts',(17.1832926155107,20.6522058852875,18.1863942407597));
#191601=CARTESIAN_POINT('Ctrl Pts',(17.1924515228629,20.6619781849337,18.18721189061));
#191602=CARTESIAN_POINT('Ctrl Pts',(17.1955507761671,20.6652638643242,18.1874868475182));
#191603=CARTESIAN_POINT('Ctrl Pts',(17.2011159217117,20.6711260633838,18.18797745277));
#191604=CARTESIAN_POINT('Ctrl Pts',(17.2035778220657,20.6737062850552,18.1881934007897));
#191605=CARTESIAN_POINT('Ctrl Pts',(17.2089219372367,20.679278980206,18.1886598162157));
#191606=CARTESIAN_POINT('Ctrl Pts',(17.2118064353551,20.6822691846401,18.1889101017006));
#191607=CARTESIAN_POINT('Ctrl Pts',(17.2198843538614,20.6905939437266,18.1896070094328));
#191608=CARTESIAN_POINT('Ctrl Pts',(17.2250971983932,20.6959096831909,18.1900521442742));
#191609=CARTESIAN_POINT('Ctrl Pts',(17.255454605516,20.726541371441,18.1926187489927));
#191610=CARTESIAN_POINT('Ctrl Pts',(17.281209555976,20.7512475116724,18.194695001097));
#191611=CARTESIAN_POINT('Ctrl Pts',(17.3658493623777,20.828427487669,18.2012494845455));
#191612=CARTESIAN_POINT('Ctrl Pts',(17.427048535344,20.8782695198108,18.2055906619453));
#191613=CARTESIAN_POINT('Ctrl Pts',(17.5646212964521,20.9780709037051,18.2148598840472));
#191614=CARTESIAN_POINT('Ctrl Pts',(17.6417263091053,21.026743426643,18.2197669245028));
#191615=CARTESIAN_POINT('Ctrl Pts',(17.8150509427724,21.1211080523016,18.2306130365245));
#191616=CARTESIAN_POINT('Ctrl Pts',(17.9120569164847,21.164813054697,18.2365759953428));
#191617=CARTESIAN_POINT('Ctrl Pts',(18.0251851485167,21.2058607629054,18.2436279209302));
#191618=CARTESIAN_POINT('Ctrl Pts',(18.0384920188413,21.2105390946066,18.2444587012989));
#191619=CARTESIAN_POINT('Ctrl Pts',(18.0597973702612,21.2177910682802,18.2457913157012));
#191620=CARTESIAN_POINT('Ctrl Pts',(18.0677662835199,21.2204507233563,18.2462903043328));
#191621=CARTESIAN_POINT('Ctrl Pts',(18.0818792508801,21.2250678010382,18.2471750640675));
#191622=CARTESIAN_POINT('Ctrl Pts',(18.0880168470452,21.2270447275024,18.2475601867311));
#191623=CARTESIAN_POINT('Ctrl Pts',(18.1007601273753,21.2310851854218,18.2483605671249));
#191624=CARTESIAN_POINT('Ctrl Pts',(18.1073670820502,21.2331444253601,18.2487759605331));
#191625=CARTESIAN_POINT('Ctrl Pts',(18.1244158141738,21.2383665564719,18.2498489969937));
#191626=CARTESIAN_POINT('Ctrl Pts',(18.1348720626799,21.2414811601326,18.250508211446));
#191627=CARTESIAN_POINT('Ctrl Pts',(18.1791643279064,21.2543025884172,18.2533055846432));
#191628=CARTESIAN_POINT('Ctrl Pts',(18.2132140304609,21.2632450709468,18.2554684022502));
#191629=CARTESIAN_POINT('Ctrl Pts',(18.3030415831973,21.2844570968317,18.2612097600631));
#191630=CARTESIAN_POINT('Ctrl Pts',(18.3591177588786,21.2953252835938,18.2648299836604));
#191631=CARTESIAN_POINT('Ctrl Pts',(18.5659272519748,21.3267915790369,18.2782974683967));
#191632=CARTESIAN_POINT('Ctrl Pts',(18.718316899986,21.3333971617287,18.2884831801166));
#191633=CARTESIAN_POINT('Ctrl Pts',(18.8925927867251,21.3221718057037,18.2998897881684));
#191634=CARTESIAN_POINT('Ctrl Pts',(18.9150845518902,21.3203616334931,18.3013563073899));
#191635=CARTESIAN_POINT('Ctrl Pts',(18.9886351993013,21.3132570303254,18.3061255942552));
#191636=CARTESIAN_POINT('Ctrl Pts',(19.0395351343045,21.3064648466792,18.3093846065088));
#191637=CARTESIAN_POINT('Ctrl Pts',(19.0979042913866,21.296503458526,18.3130367114465));
#191638=CARTESIAN_POINT('Ctrl Pts',(19.1056593158684,21.2951354001472,18.3135201822506));
#191639=CARTESIAN_POINT('Ctrl Pts',(19.1180124292984,21.2928850523483,18.3142873155793));
#191640=CARTESIAN_POINT('Ctrl Pts',(19.1226154509021,21.2920307420452,18.3145725003787));
#191641=CARTESIAN_POINT('Ctrl Pts',(19.1307460429651,21.2904938053331,18.3150750176731));
#191642=CARTESIAN_POINT('Ctrl Pts',(19.134274757541,21.2898174590978,18.315292703696));
#191643=CARTESIAN_POINT('Ctrl Pts',(19.1417317873122,21.2883684838018,18.3157518476623));
#191644=CARTESIAN_POINT('Ctrl Pts',(19.14565963046,21.2875936957285,18.3159931809005));
#191645=CARTESIAN_POINT('Ctrl Pts',(19.1562137238959,21.2854807226222,18.3166403226643));
#191646=CARTESIAN_POINT('Ctrl Pts',(19.1628358662414,21.2841219211182,18.3170449704413));
#191647=CARTESIAN_POINT('Ctrl Pts',(19.195151363831,21.2773296161408,18.3190132744816));
#191648=CARTESIAN_POINT('Ctrl Pts',(19.2207498426422,21.2714498044258,18.3205528397991));
#191649=CARTESIAN_POINT('Ctrl Pts',(19.2937720852216,21.2532401077807,18.3249053749511));
#191650=CARTESIAN_POINT('Ctrl Pts',(19.3408879592056,21.2397378051114,18.3276660300718));
#191651=CARTESIAN_POINT('Ctrl Pts',(19.4793729662792,21.1947940102237,18.3357496452728));
#191652=CARTESIAN_POINT('Ctrl Pts',(19.5691050828594,21.1587218701743,18.3409511662204));
#191653=CARTESIAN_POINT('Ctrl Pts',(19.7830122397995,21.0552211243247,18.3538817866873));
#191654=CARTESIAN_POINT('Ctrl Pts',(19.9034877900003,20.9812737111969,18.3616606841721));
#191655=CARTESIAN_POINT('Ctrl Pts',(20.0270785078051,20.8872580288922,18.3707579161789));
#191656=CARTESIAN_POINT('Ctrl Pts',(20.0383583019562,20.8784958506703,18.3715990288217));
#191657=CARTESIAN_POINT('Ctrl Pts',(20.0561708874211,20.86436765215,18.3729450942776));
#191658=CARTESIAN_POINT('Ctrl Pts',(20.0627618151563,20.8590753878817,18.3734471094479));
#191659=CARTESIAN_POINT('Ctrl Pts',(20.0743309016171,20.8496713400315,18.3743353873944));
#191660=CARTESIAN_POINT('Ctrl Pts',(20.0793223030421,20.8455759651918,18.3747209847905));
#191661=CARTESIAN_POINT('Ctrl Pts',(20.0896082653568,20.8370574488203,18.3755205321053));
#191662=CARTESIAN_POINT('Ctrl Pts',(20.0949000892878,20.8326311359836,18.3759346087247));
#191663=CARTESIAN_POINT('Ctrl Pts',(20.1084298949,20.8212013465263,18.3770003949));
#191664=CARTESIAN_POINT('Ctrl Pts',(20.116635952907,20.814160543204,18.3776536354871));
#191665=CARTESIAN_POINT('Ctrl Pts',(20.1506772402487,20.784497322077,18.3803924556932));
#191666=CARTESIAN_POINT('Ctrl Pts',(20.1760128535243,20.7613118844096,18.3825014255533));
#191667=CARTESIAN_POINT('Ctrl Pts',(20.2405626244418,20.6992886434286,18.3880658515075));
#191668=CARTESIAN_POINT('Ctrl Pts',(20.2788399216034,20.6595174558916,18.3915598646953));
#191669=CARTESIAN_POINT('Ctrl Pts',(20.3882818318116,20.536527037678,18.4021427062645));
#191670=CARTESIAN_POINT('Ctrl Pts',(20.4545894559892,20.4492401893505,18.4093798808806));
#191671=CARTESIAN_POINT('Ctrl Pts',(20.5426730035151,20.3124651811051,18.4201261952941));
#191672=CARTESIAN_POINT('Ctrl Pts',(20.5698016848622,20.2666306595719,18.4236353136285));
#191673=CARTESIAN_POINT('Ctrl Pts',(20.6009789285807,20.2091117480658,18.4278934234894));
#191674=CARTESIAN_POINT('Ctrl Pts',(20.6066912146194,20.198352522856,18.4286838262523));
#191675=CARTESIAN_POINT('Ctrl Pts',(20.637139710341,20.13978711272,18.432951190868));
#191676=CARTESIAN_POINT('Ctrl Pts',(20.6601409685388,20.0910956134165,18.4363738886176));
#191677=CARTESIAN_POINT('Ctrl Pts',(20.6846909389624,20.0335388798155,18.4402340422234));
#191678=CARTESIAN_POINT('Ctrl Pts',(20.6880693495739,20.0254804056937,18.4407703510372));
#191679=CARTESIAN_POINT('Ctrl Pts',(20.6931070014911,20.0132523852791,18.4415776351982));
#191680=CARTESIAN_POINT('Ctrl Pts',(20.6948029916941,20.0090982155089,18.4418507576983));
#191681=CARTESIAN_POINT('Ctrl Pts',(20.6978224474137,20.001634617435,18.4423393931503));
#191682=CARTESIAN_POINT('Ctrl Pts',(20.6991507687937,19.9983272253324,18.4425551955531));
#191683=CARTESIAN_POINT('Ctrl Pts',(20.7020176287673,19.9911365642681,18.443022787671));
#191684=CARTESIAN_POINT('Ctrl Pts',(20.7035530247087,19.9872521044091,18.4432743874316));
#191685=CARTESIAN_POINT('Ctrl Pts',(20.7078303174843,19.9763364181887,18.4439786765076));
#191686=CARTESIAN_POINT('Ctrl Pts',(20.7105461590321,19.9692949560225,18.4444298269297));
#191687=CARTESIAN_POINT('Ctrl Pts',(20.7264927428894,19.9272818726399,18.4471036398129));
#191688=CARTESIAN_POINT('Ctrl Pts',(20.7388336321318,19.8919769054545,18.4492765532668));
#191689=CARTESIAN_POINT('Ctrl Pts',(20.7762416755458,19.7751069186339,18.456285751501));
#191690=CARTESIAN_POINT('Ctrl Pts',(20.7973162790691,19.6923480108486,18.4609621616113));
#191691=CARTESIAN_POINT('Ctrl Pts',(20.8467478729529,19.433793505942,18.4752908852577));
#191692=CARTESIAN_POINT('Ctrl Pts',(20.8579935547105,19.255556975611,18.4848437177853));
#191693=CARTESIAN_POINT('Ctrl Pts',(20.8453865527207,19.0552567752956,18.4965080512658));
#191694=CARTESIAN_POINT('Ctrl Pts',(20.8435862765752,19.0325208436504,18.497844335318));
#191695=CARTESIAN_POINT('Ctrl Pts',(20.8405147972411,19.0003463530487,18.4997544878449));
#191696=CARTESIAN_POINT('Ctrl Pts',(20.8395466552243,18.9908799687692,18.5003188428228));
#191697=CARTESIAN_POINT('Ctrl Pts',(20.8378682528908,18.9754943476607,18.5012400251024));
#191698=CARTESIAN_POINT('Ctrl Pts',(20.8371967456192,18.9695709505824,18.5015956279512));
#191699=CARTESIAN_POINT('Ctrl Pts',(20.8357373280767,18.9571657267569,18.5023423866502));
#191700=CARTESIAN_POINT('Ctrl Pts',(20.8349444316096,18.9506845599857,18.5027336962554));
#191701=CARTESIAN_POINT('Ctrl Pts',(20.8329839852107,18.935252449023,18.5036682472012));
#191702=CARTESIAN_POINT('Ctrl Pts',(20.8317891513394,18.9263051552649,18.5042123452468));
#191703=CARTESIAN_POINT('Ctrl Pts',(20.8275561403065,18.8960816070693,18.5060580797892));
#191704=CARTESIAN_POINT('Ctrl Pts',(20.8242512778151,18.8748446059281,18.5073681118313));
#191705=CARTESIAN_POINT('Ctrl Pts',(20.7903457929804,18.6768583042241,18.5197078120399));
#191706=CARTESIAN_POINT('Ctrl Pts',(20.73772467273,18.5046519942206,18.5314807501534));
#191707=CARTESIAN_POINT('Ctrl Pts',(20.6145053173395,18.2312396779801,18.5512939042678));
#191708=CARTESIAN_POINT('Ctrl Pts',(20.5556497141551,18.1257214266051,18.5592315852164));
#191709=CARTESIAN_POINT('Ctrl Pts',(20.4828072967564,18.0179148619257,18.5672674139715));
#191710=CARTESIAN_POINT('Ctrl Pts',(20.477439876999,18.010085135871,18.5678505137086));
#191711=CARTESIAN_POINT('Ctrl Pts',(20.4694049094193,17.9985315358726,18.5687098421683));
#191712=CARTESIAN_POINT('Ctrl Pts',(20.4667777354081,17.9947799143557,18.5689887053815));
#191713=CARTESIAN_POINT('Ctrl Pts',(20.4620801068341,17.9881177891895,18.5694835579186));
#191714=CARTESIAN_POINT('Ctrl Pts',(20.4600144454931,17.9852039762845,18.5696998686232));
#191715=CARTESIAN_POINT('Ctrl Pts',(20.4555555970028,17.9789479624314,18.5701640189079));
#191716=CARTESIAN_POINT('Ctrl Pts',(20.4531600542267,17.9756075095498,18.5704116927634));
#191717=CARTESIAN_POINT('Ctrl Pts',(20.4465162232933,17.9663998004366,18.5710939992904));
#191718=CARTESIAN_POINT('Ctrl Pts',(20.4422474813891,17.9605472749548,18.5715272440639));
#191719=CARTESIAN_POINT('Ctrl Pts',(20.4186218522516,17.9285028628964,18.573897678806));
#191720=CARTESIAN_POINT('Ctrl Pts',(20.3986914371649,17.9027368867428,18.575797351968));
#191721=CARTESIAN_POINT('Ctrl Pts',(20.2757125870309,17.7511138193147,18.5870061519822));
#191722=CARTESIAN_POINT('Ctrl Pts',(20.1590242846884,17.6370041360469,18.5956034784095));
#191723=CARTESIAN_POINT('Ctrl Pts',(19.9380209488694,17.4658126054789,18.6109075402293));
#191724=CARTESIAN_POINT('Ctrl Pts',(19.8398805650126,17.4020311229246,18.6174314177453));
#191725=CARTESIAN_POINT('Ctrl Pts',(19.7244191993803,17.3399140882788,18.6251124701548));
#191726=CARTESIAN_POINT('Ctrl Pts',(19.7117831477673,17.3332798982191,18.625952917221));
#191727=CARTESIAN_POINT('Ctrl Pts',(19.6915608505614,17.3229222447065,18.6272981165492));
#191728=CARTESIAN_POINT('Ctrl Pts',(19.6840175829805,17.3191154946899,18.6277999371518));
#191729=CARTESIAN_POINT('Ctrl Pts',(19.6706708857595,17.3124799629136,18.6286879885203));
#191730=CARTESIAN_POINT('Ctrl Pts',(19.6648768938411,17.3096323641821,18.6290735549969));
#191731=CARTESIAN_POINT('Ctrl Pts',(19.6528633353563,17.3037960818025,18.6298731538759));
#191732=CARTESIAN_POINT('Ctrl Pts',(19.6466420073641,17.3008112189391,18.6302873135494));
#191733=CARTESIAN_POINT('Ctrl Pts',(19.6306292815823,17.2932247323674,18.6313535573939));
#191734=CARTESIAN_POINT('Ctrl Pts',(19.6208170900383,17.2886676958066,18.6320071751333));
#191735=CARTESIAN_POINT('Ctrl Pts',(19.5796667597815,17.2699385242901,18.6347496561466));
#191736=CARTESIAN_POINT('Ctrl Pts',(19.5480219742388,17.2564565933254,18.6368619879219));
#191737=CARTESIAN_POINT('Ctrl Pts',(19.4646753299354,17.2233227787322,18.6424374044971));
#191738=CARTESIAN_POINT('Ctrl Pts',(19.4125095371365,17.2049164641964,18.6459392365308));
#191739=CARTESIAN_POINT('Ctrl Pts',(19.2550228870426,17.1561941485145,18.6565370893406));
#191740=CARTESIAN_POINT('Ctrl Pts',(19.1480107101045,17.1319897530977,18.6637814049215));
#191741=CARTESIAN_POINT('Ctrl Pts',(18.9810768829046,17.107635602741,18.6749249270913));
#191742=CARTESIAN_POINT('Ctrl Pts',(18.9222032790448,17.1015524895205,18.6788228337887));
#191743=CARTESIAN_POINT('Ctrl Pts',(18.8037935472515,17.094315268071,18.6865187755934));
#191744=CARTESIAN_POINT('Ctrl Pts',(18.744304140804,17.09318966923,18.6903128167868));
#191745=CARTESIAN_POINT('Ctrl Pts',(18.6758959977996,17.094778607705,18.6945356910558));
#191746=CARTESIAN_POINT('Ctrl Pts',(18.666952217849,17.0950430870013,18.6950850283632));
#191747=CARTESIAN_POINT('Ctrl Pts',(18.6534812830421,17.0955269385285,18.6959079869443));
#191748=CARTESIAN_POINT('Ctrl Pts',(18.6489528466993,17.0957041530343,18.6961838790378));
#191749=CARTESIAN_POINT('Ctrl Pts',(18.640860676204,17.0960468578927,18.6966754947986));
#191750=CARTESIAN_POINT('Ctrl Pts',(18.6372967698725,17.0962068155843,18.6968915233459));
#191751=CARTESIAN_POINT('Ctrl Pts',(18.6295941199418,17.0965720436191,18.6973573676377));
#191752=CARTESIAN_POINT('Ctrl Pts',(18.6254555824869,17.0967804559084,18.697607005447));
#191753=CARTESIAN_POINT('Ctrl Pts',(18.6139331641101,17.0973946346634,18.6983002841973));
#191754=CARTESIAN_POINT('Ctrl Pts',(18.6065506746623,17.0978269454219,18.6987424627533));
#191755=CARTESIAN_POINT('Ctrl Pts',(18.5643658561525,17.1005191181522,18.7012584247532));
#191756=CARTESIAN_POINT('Ctrl Pts',(18.529619128739,17.1036001629456,18.7032890514265));
#191757=CARTESIAN_POINT('Ctrl Pts',(18.4195022309583,17.1161138704015,18.7096361156139));
#191758=CARTESIAN_POINT('Ctrl Pts',(18.3445522496515,17.1287442579842,18.7138253050929));
#191759=CARTESIAN_POINT('Ctrl Pts',(18.1744392097267,17.1669205804375,18.7233438065338));
#191760=CARTESIAN_POINT('Ctrl Pts',(18.0800600090312,17.1951301249886,18.7286362770021));
#191761=CARTESIAN_POINT('Ctrl Pts',(17.8917257986939,17.2660468443853,18.7397119167156));
#191762=CARTESIAN_POINT('Ctrl Pts',(17.7982479124415,17.3092553546494,18.7454933415189));
#191763=CARTESIAN_POINT('Ctrl Pts',(17.6949024064275,17.3664948393134,18.7524163990381));
#191764=CARTESIAN_POINT('Ctrl Pts',(17.6815990441225,17.374052720817,18.7533180106836));
#191765=CARTESIAN_POINT('Ctrl Pts',(17.6614319006682,17.3858010209012,18.7547013154574));
#191766=CARTESIAN_POINT('Ctrl Pts',(17.6545079581591,17.3898875460632,18.755179249551));
#191767=CARTESIAN_POINT('Ctrl Pts',(17.6422722633395,17.3972033768201,18.7560292580482));
#191768=CARTESIAN_POINT('Ctrl Pts',(17.6369511133171,17.4004168397428,18.75640075079));
#191769=CARTESIAN_POINT('Ctrl Pts',(17.6256915133991,17.4072844138341,18.7571907726096));
#191770=CARTESIAN_POINT('Ctrl Pts',(17.6197568199446,17.4109445144278,18.7576095189449));
#191771=CARTESIAN_POINT('Ctrl Pts',(17.6076380683345,17.4185014015234,18.7584694650207));
#191772=CARTESIAN_POINT('Ctrl Pts',(17.6014558993608,17.4224010274365,18.7589107661908));
#191773=CARTESIAN_POINT('Ctrl Pts',(17.5861792008668,17.432148314861,18.7600078201595));
#191774=CARTESIAN_POINT('Ctrl Pts',(17.5771091164892,17.4380337336869,18.760664972019));
#191775=CARTESIAN_POINT('Ctrl Pts',(17.4618289665899,17.5140982533416,18.7690926509832));
#191776=CARTESIAN_POINT('Ctrl Pts',(17.3621323002869,17.5936368096121,18.7772270133833));
#191777=CARTESIAN_POINT('Ctrl Pts',(17.1693316058984,17.7781723023871,18.7947151941702));
#191778=CARTESIAN_POINT('Ctrl Pts',(17.0782666057596,17.8844519064824,18.8040697644315));
#191779=CARTESIAN_POINT('Ctrl Pts',(16.9730966445309,18.0350534162858,18.8158636918841));
#191780=CARTESIAN_POINT('Ctrl Pts',(16.9489979196492,18.0719656773321,18.8186490011286));
#191781=CARTESIAN_POINT('Ctrl Pts',(16.9221428448272,18.1160481514842,18.8218304611239));
#191782=CARTESIAN_POINT('Ctrl Pts',(16.9182527490838,18.1225112191654,18.8222933463612));
#191783=CARTESIAN_POINT('Ctrl Pts',(16.9120541681013,18.1329353445121,18.8230340459933));
#191784=CARTESIAN_POINT('Ctrl Pts',(16.9097238995672,18.1368832809758,18.8233132260267));
#191785=CARTESIAN_POINT('Ctrl Pts',(16.905596592062,18.1439279329991,18.8238089559392));
#191786=CARTESIAN_POINT('Ctrl Pts',(16.9037945655925,18.1470216699099,18.8240258268366));
#191787=CARTESIAN_POINT('Ctrl Pts',(16.8999660993169,18.1536329257218,18.8244874865521));
#191788=CARTESIAN_POINT('Ctrl Pts',(16.8979419308249,18.1571516969334,18.8247321289133));
#191789=CARTESIAN_POINT('Ctrl Pts',(16.89244908921,18.1667641993224,18.8253975816574));
#191790=CARTESIAN_POINT('Ctrl Pts',(16.8890005134409,18.1728694387596,18.8258171151877));
#191791=CARTESIAN_POINT('Ctrl Pts',(16.8712703330513,18.2046257557163,18.8279837742874));
#191792=CARTESIAN_POINT('Ctrl Pts',(16.8574923532728,18.2305561313607,18.8297005802777));
#191793=CARTESIAN_POINT('Ctrl Pts',(16.8181649353578,18.3084392362931,18.8347281266977));
#191794=CARTESIAN_POINT('Ctrl Pts',(16.7942008718324,18.3611645926916,18.837965108499));
#191795=CARTESIAN_POINT('Ctrl Pts',(16.6940055028755,18.6080157288271,18.8526529722907));
#191796=CARTESIAN_POINT('Ctrl Pts',(16.6445611156937,18.8117328808028,18.8636104206104));
#191797=CARTESIAN_POINT('Ctrl Pts',(16.6232302280078,19.046446771021,18.8772499189784));
#191798=CARTESIAN_POINT('Ctrl Pts',(16.621292764556,19.0735415207636,18.8788369296319));
#191799=CARTESIAN_POINT('Ctrl Pts',(16.6193445967681,19.110870313191,18.8810434756792));
#191800=CARTESIAN_POINT('Ctrl Pts',(16.6188859028633,19.1210790394894,18.8816489840458));
#191801=CARTESIAN_POINT('Ctrl Pts',(16.618271724327,19.1373794158982,18.8826192367807));
#191802=CARTESIAN_POINT('Ctrl Pts',(16.6180685938414,19.1434691912992,18.8829824843594));
#191803=CARTESIAN_POINT('Ctrl Pts',(16.6177137006869,19.1556923160984,18.8837131460156));
#191804=CARTESIAN_POINT('Ctrl Pts',(16.6175623044106,19.161825616239,18.8840805679802));
#191805=CARTESIAN_POINT('Ctrl Pts',(16.6172825438745,19.1755831188097,18.8849065375177));
#191806=CARTESIAN_POINT('Ctrl Pts',(16.6171687078969,19.1832075021295,18.885365536024));
#191807=CARTESIAN_POINT('Ctrl Pts',(16.6170306367634,19.1977001167314,18.8862404348957));
#191808=CARTESIAN_POINT('Ctrl Pts',(16.6169986298215,19.2045681769785,18.8866560843466));
#191809=CARTESIAN_POINT('Ctrl Pts',(16.6170000449378,19.2114361958265,18.8870727828678));
#191810=CARTESIAN_POINT('Ctrl Pts',(16.6170000447709,19.2114353848898,18.8870727336665));
#191811=CARTESIAN_POINT('Ctrl Pts',(16.6170021622649,19.2217314122616,18.8876974172358));
#191812=CARTESIAN_POINT('Ctrl Pts',(16.6170793917548,19.2320271783322,18.8883244488401));
#191813=CARTESIAN_POINT('Ctrl Pts',(16.61753901209,19.2630888551937,18.8902234410339));
#191814=CARTESIAN_POINT('Ctrl Pts',(16.6181518837126,19.2838495921527,18.8915025022528));
#191815=CARTESIAN_POINT('Ctrl Pts',(16.6269496222173,19.4826435974031,18.9038465954591));
#191816=CARTESIAN_POINT('Ctrl Pts',(16.6572801772349,19.658954821958,18.9156267936816));
#191817=CARTESIAN_POINT('Ctrl Pts',(16.7203860615788,19.8655869711512,18.9298814848752));
#191818=CARTESIAN_POINT('Ctrl Pts',(16.7324248545875,19.9015224718576,18.9323739729723));
#191819=CARTESIAN_POINT('Ctrl Pts',(16.7454193714968,19.9371102422787,18.9348454715054));
#191820=CARTESIAN_POINT('Origin',(18.734,19.211,0.));
#191821=CARTESIAN_POINT('',(16.7454193617555,19.9371102156003,19.9537492222746));
#191822=CARTESIAN_POINT('',(16.7454193946088,19.9371103055747,19.7345260524097));
#191823=CARTESIAN_POINT('',(16.7454193623258,19.9371102171621,0.));
#191824=CARTESIAN_POINT('',(16.620085879662,19.211828459305,19.9109956432659));
#191825=CARTESIAN_POINT('Ctrl Pts',(16.7454193617555,19.9371102156003,19.9537492222746));
#191826=CARTESIAN_POINT('Ctrl Pts',(16.7274346612152,19.8878559474318,19.9507625090015));
#191827=CARTESIAN_POINT('Ctrl Pts',(16.711283767598,19.8379440837176,19.9478475408055));
#191828=CARTESIAN_POINT('Ctrl Pts',(16.6439835662993,19.6001371164755,19.9342646372123));
#191829=CARTESIAN_POINT('Ctrl Pts',(16.6170670033202,19.4064030010435,19.9239833213256));
#191830=CARTESIAN_POINT('Ctrl Pts',(16.617000124922,19.2117272686678,19.9127739632071));
#191831=CARTESIAN_POINT('Ctrl Pts',(16.7477767826476,19.936270776259,19.1554367658253));
#191832=CARTESIAN_POINT('Ctrl Pts',(16.835152879605,20.1806248752966,19.1710019282197));
#191833=CARTESIAN_POINT('Ctrl Pts',(17.3199689711641,21.0303283365173,19.2289590261745));
#191834=CARTESIAN_POINT('Ctrl Pts',(19.0938031815268,21.6882711475642,19.3293080596899));
#191835=CARTESIAN_POINT('Ctrl Pts',(21.0117476411797,20.2493623677241,19.4564838663713));
#191836=CARTESIAN_POINT('Ctrl Pts',(20.8400000149027,17.8578205193086,19.5836596730528));
#191837=CARTESIAN_POINT('Ctrl Pts',(18.7361280844105,16.7077369418621,19.7108354797341));
#191838=CARTESIAN_POINT('Ctrl Pts',(16.9296977525301,17.6912382419271,19.8199301623757));
#191839=CARTESIAN_POINT('Ctrl Pts',(16.6216054888487,18.8061996502611,19.8866329094569));
#191840=CARTESIAN_POINT('Ctrl Pts',(16.620175975625,19.2118314138068,19.9109437209775));
#191841=CARTESIAN_POINT('Ctrl Pts',(16.7454193714968,19.9371102422787,18.9348454715054));
#191842=CARTESIAN_POINT('Ctrl Pts',(16.7585801455699,19.9731533371889,18.9373485914015));
#191843=CARTESIAN_POINT('Ctrl Pts',(16.7727212540933,20.008839748599,18.9398301656811));
#191844=CARTESIAN_POINT('Ctrl Pts',(16.8015898582272,20.0762761626567,18.9445019017568));
#191845=CARTESIAN_POINT('Ctrl Pts',(16.8161467769515,20.1080792261891,18.9466972924739));
#191846=CARTESIAN_POINT('Ctrl Pts',(16.8347318678157,20.146160058031,18.9493038779225));
#191847=CARTESIAN_POINT('Ctrl Pts',(16.8380127503703,20.1527940990628,18.9497571382522));
#191848=CARTESIAN_POINT('Ctrl Pts',(16.8431853658365,20.1631166947162,18.9504609528935));
#191849=CARTESIAN_POINT('Ctrl Pts',(16.8450532193502,20.1668170545023,18.9507129562211));
#191850=CARTESIAN_POINT('Ctrl Pts',(16.848548828532,20.1736918542105,18.9511805641631));
#191851=CARTESIAN_POINT('Ctrl Pts',(16.8501737235963,20.1768676341751,18.9513963373115));
#191852=CARTESIAN_POINT('Ctrl Pts',(16.8538802699165,20.1840669668173,18.9518849621267));
#191853=CARTESIAN_POINT('Ctrl Pts',(16.8559668079206,20.1880879447033,18.9521575018739));
#191854=CARTESIAN_POINT('Ctrl Pts',(16.8622089495612,20.2000233411172,18.952965474331));
#191855=CARTESIAN_POINT('Ctrl Pts',(16.8664018512445,20.2079182849687,18.953498611539));
#191856=CARTESIAN_POINT('Ctrl Pts',(16.8987523988646,20.2679116849539,18.9575416544899));
#191857=CARTESIAN_POINT('Ctrl Pts',(16.9290377073851,20.3188395825676,18.960926348901));
#191858=CARTESIAN_POINT('Ctrl Pts',(17.0709023836289,20.5361012589682,18.9754504885729));
#191859=CARTESIAN_POINT('Ctrl Pts',(17.2036165909359,20.6873886003564,18.9858918624293));
#191860=CARTESIAN_POINT('Ctrl Pts',(17.3974419635339,20.8536618643551,19.0003465948215));
#191861=CARTESIAN_POINT('Ctrl Pts',(17.440646787567,20.8878906016631,19.0035195065488));
#191862=CARTESIAN_POINT('Ctrl Pts',(17.4925426493952,20.9258051810881,19.0072998698884));
#191863=CARTESIAN_POINT('Ctrl Pts',(17.4999853085875,20.9311688579501,19.0078412982107));
#191864=CARTESIAN_POINT('Ctrl Pts',(17.5142302202002,20.9412946654857,19.0088763111339));
#191865=CARTESIAN_POINT('Ctrl Pts',(17.5210261011059,20.9460654923446,19.0093695513505));
#191866=CARTESIAN_POINT('Ctrl Pts',(17.533045020102,20.9543978601523,19.0102410150682));
#191867=CARTESIAN_POINT('Ctrl Pts',(17.5382563028456,20.9579762367882,19.0106185907259));
#191868=CARTESIAN_POINT('Ctrl Pts',(17.5485073269588,20.9649478426138,19.0113607979005));
#191869=CARTESIAN_POINT('Ctrl Pts',(17.5535458058536,20.9683428256232,19.0117253579882));
#191870=CARTESIAN_POINT('Ctrl Pts',(17.5656263519771,20.9764074358049,19.0125989070148));
#191871=CARTESIAN_POINT('Ctrl Pts',(17.5726818581997,20.981056656177,19.0131086570988));
#191872=CARTESIAN_POINT('Ctrl Pts',(17.5982467684564,20.997683986732,19.0149542436543));
#191873=CARTESIAN_POINT('Ctrl Pts',(17.6169146811909,21.0094146919493,19.0162992320329));
#191874=CARTESIAN_POINT('Ctrl Pts',(17.7949162185152,21.1174280242474,19.0291029593766));
#191875=CARTESIAN_POINT('Ctrl Pts',(17.9660863529535,21.1925718334782,19.0413666858505));
#191876=CARTESIAN_POINT('Ctrl Pts',(18.2214554473875,21.2665662278038,19.0589192011326));
#191877=CARTESIAN_POINT('Ctrl Pts',(18.2992863674331,21.2844223395579,19.0641603309251));
#191878=CARTESIAN_POINT('Ctrl Pts',(18.4133637890882,21.3038861651082,19.0715367863243));
#191879=CARTESIAN_POINT('Ctrl Pts',(18.4489341675892,21.3090271462841,19.0737941187758));
#191880=CARTESIAN_POINT('Ctrl Pts',(18.4920288750255,21.3141392324147,19.0764639576536));
#191881=CARTESIAN_POINT('Ctrl Pts',(18.4994419650273,21.3149788944479,19.076920904734));
#191882=CARTESIAN_POINT('Ctrl Pts',(18.5109934642135,21.3162254924305,19.0776291794747));
#191883=CARTESIAN_POINT('Ctrl Pts',(18.5151288104673,21.3166594435146,19.0778819855174));
#191884=CARTESIAN_POINT('Ctrl Pts',(18.5228130357383,21.317442921688,19.0783503168764));
#191885=CARTESIAN_POINT('Ctrl Pts',(18.5263614855395,21.3177956625623,19.0785660154931));
#191886=CARTESIAN_POINT('Ctrl Pts',(18.5344020118421,21.3185744358125,19.0790534972824));
#191887=CARTESIAN_POINT('Ctrl Pts',(18.5388945577166,21.318995072723,19.0793249745745));
#191888=CARTESIAN_POINT('Ctrl Pts',(18.5522075302532,21.3201986415674,19.0801268892954));
#191889=CARTESIAN_POINT('Ctrl Pts',(18.5610316884447,21.3209406107836,19.0806550819175));
#191890=CARTESIAN_POINT('Ctrl Pts',(18.6265559244888,21.3260363097504,19.084554172067));
#191891=CARTESIAN_POINT('Ctrl Pts',(18.6834115366662,21.3281596160968,19.0878097049991));
#191892=CARTESIAN_POINT('Ctrl Pts',(18.8919307797714,21.3275401986158,19.0995029860789));
#191893=CARTESIAN_POINT('Ctrl Pts',(19.0430921722761,21.3107981313767,19.1075312893274));
#191894=CARTESIAN_POINT('Ctrl Pts',(19.2817209477189,21.2580198864463,19.1209921795625));
#191895=CARTESIAN_POINT('Ctrl Pts',(19.3708436865335,21.2320680080381,19.1261994000153));
#191896=CARTESIAN_POINT('Ctrl Pts',(19.4777737216926,21.193153798485,19.132827613407));
#191897=CARTESIAN_POINT('Ctrl Pts',(19.4974659976883,21.1856525398362,19.1340643357322));
#191898=CARTESIAN_POINT('Ctrl Pts',(19.5253629264923,21.174546261387,19.1358406773342));
#191899=CARTESIAN_POINT('Ctrl Pts',(19.5336621393182,21.1711810276657,19.1363722330577));
#191900=CARTESIAN_POINT('Ctrl Pts',(19.5479630240476,21.1652762501154,19.1372936648727));
#191901=CARTESIAN_POINT('Ctrl Pts',(19.5539748258749,21.1627614479615,19.1376826985251));
#191902=CARTESIAN_POINT('Ctrl Pts',(19.5654775095669,21.1578872250532,19.1384303270526));
#191903=CARTESIAN_POINT('Ctrl Pts',(19.570970206988,21.1555322284465,19.1387887682277));
#191904=CARTESIAN_POINT('Ctrl Pts',(19.5852581125548,21.1493345293332,19.1397249559992));
#191905=CARTESIAN_POINT('Ctrl Pts',(19.5940372166824,21.1454552470841,19.1403039495925));
#191906=CARTESIAN_POINT('Ctrl Pts',(19.6240420362155,21.1319521904511,19.1422959109654));
#191907=CARTESIAN_POINT('Ctrl Pts',(19.6451344606136,21.1220379563974,19.1437188249316));
#191908=CARTESIAN_POINT('Ctrl Pts',(19.8194757360087,21.036548623844,19.1556742181414));
#191909=CARTESIAN_POINT('Ctrl Pts',(19.9631935520853,20.9430354670292,19.1668692990661));
#191910=CARTESIAN_POINT('Ctrl Pts',(20.163275311066,20.7752931537508,19.1841228700873));
#191911=CARTESIAN_POINT('Ctrl Pts',(20.2286876589771,20.7129160372257,19.1900816354081));
#191912=CARTESIAN_POINT('Ctrl Pts',(20.3161222087,20.6181500885464,19.1983195648311));
#191913=CARTESIAN_POINT('Ctrl Pts',(20.3415437868181,20.5890368150142,19.2007514439698));
#191914=CARTESIAN_POINT('Ctrl Pts',(20.3710073540054,20.553368784506,19.2035985726797));
#191915=CARTESIAN_POINT('Ctrl Pts',(20.375827200553,20.5474694079019,19.2040652798183));
#191916=CARTESIAN_POINT('Ctrl Pts',(20.3832500207663,20.5382832944963,19.2047853508607));
#191917=CARTESIAN_POINT('Ctrl Pts',(20.3858751951312,20.5350146960136,19.2050402720945));
#191918=CARTESIAN_POINT('Ctrl Pts',(20.3907134801515,20.5289537697198,19.2055105467556));
#191919=CARTESIAN_POINT('Ctrl Pts',(20.3929292327542,20.5261636762991,19.2057260859543));
#191920=CARTESIAN_POINT('Ctrl Pts',(20.3979072400023,20.5198627322616,19.2062107240824));
#191921=CARTESIAN_POINT('Ctrl Pts',(20.4006654241092,20.5163487350725,19.2064795323371));
#191922=CARTESIAN_POINT('Ctrl Pts',(20.4087290697404,20.5060082204455,19.2072663233106));
#191923=CARTESIAN_POINT('Ctrl Pts',(20.4140039335281,20.4991578075568,19.2077821853406));
#191924=CARTESIAN_POINT('Ctrl Pts',(20.4504840553929,20.4511761982057,19.2113595949867));
#191925=CARTESIAN_POINT('Ctrl Pts',(20.4802202107964,20.4089442489124,19.2143262493077));
#191926=CARTESIAN_POINT('Ctrl Pts',(20.5938196131342,20.2343747626169,19.2260563218993));
#191927=CARTESIAN_POINT('Ctrl Pts',(20.6644243904402,20.0940025802169,19.2343354390815));
#191928=CARTESIAN_POINT('Ctrl Pts',(20.7513203842857,19.8596922831932,19.2480963203755));
#191929=CARTESIAN_POINT('Ctrl Pts',(20.7779278710348,19.7702308594589,19.25333061389));
#191930=CARTESIAN_POINT('Ctrl Pts',(20.8032262249534,19.6587035343242,19.259991594395));
#191931=CARTESIAN_POINT('Ctrl Pts',(20.8075922762007,19.6380253495216,19.2612318716746));
#191932=CARTESIAN_POINT('Ctrl Pts',(20.8133686373703,19.6084864271854,19.2630124352959));
#191933=CARTESIAN_POINT('Ctrl Pts',(20.8150334230137,19.5996763157297,19.2635446047835));
#191934=CARTESIAN_POINT('Ctrl Pts',(20.817811795883,19.5844432890972,19.2644667621255));
#191935=CARTESIAN_POINT('Ctrl Pts',(20.8189517837562,19.578025269946,19.2648559039174));
#191936=CARTESIAN_POINT('Ctrl Pts',(20.8210796981587,19.5657154107885,19.2656035028531));
#191937=CARTESIAN_POINT('Ctrl Pts',(20.8220723633208,19.559824445124,19.2659618051557));
#191938=CARTESIAN_POINT('Ctrl Pts',(20.8245928406269,19.5444703283729,19.2668971051403));
#191939=CARTESIAN_POINT('Ctrl Pts',(20.8260813251085,19.5350009407245,19.2674753451747));
#191940=CARTESIAN_POINT('Ctrl Pts',(20.8309568445244,19.5025487437142,19.2694620086315));
#191941=CARTESIAN_POINT('Ctrl Pts',(20.8340297689101,19.4795210978309,19.2708803071689));
#191942=CARTESIAN_POINT('Ctrl Pts',(20.8566712892558,19.2855541510819,19.2829032001196));
#191943=CARTESIAN_POINT('Ctrl Pts',(20.8557080873532,19.1128960935249,19.2941807801964));
#191944=CARTESIAN_POINT('Ctrl Pts',(20.8225257674408,18.8535806484862,19.3114560055292));
#191945=CARTESIAN_POINT('Ctrl Pts',(20.8055620072477,18.7656672026526,19.3173566856285));
#191946=CARTESIAN_POINT('Ctrl Pts',(20.7734306829032,18.641888048593,19.3255255834195));
#191947=CARTESIAN_POINT('Ctrl Pts',(20.7627627904003,18.6049571859185,19.327943955215));
#191948=CARTESIAN_POINT('Ctrl Pts',(20.7487855197581,18.5610875733975,19.3307774126211));
#191949=CARTESIAN_POINT('Ctrl Pts',(20.7464374254655,18.5538527824783,19.3312433958096));
#191950=CARTESIAN_POINT('Ctrl Pts',(20.7427355112127,18.5426526355085,19.3319625924328));
#191951=CARTESIAN_POINT('Ctrl Pts',(20.7414088538667,18.5386784640151,19.3322173572816));
#191952=CARTESIAN_POINT('Ctrl Pts',(20.738932127636,18.5313318019756,19.3326874865056));
#191953=CARTESIAN_POINT('Ctrl Pts',(20.7377853524391,18.527958304721,19.3329030357343));
#191954=CARTESIAN_POINT('Ctrl Pts',(20.7351805794009,18.5203587959934,19.3333878761254));
#191955=CARTESIAN_POINT('Ctrl Pts',(20.7337177140957,18.5161345102697,19.3336568755223));
#191956=CARTESIAN_POINT('Ctrl Pts',(20.7293815173173,18.5037400714216,19.3344447452187));
#191957=CARTESIAN_POINT('Ctrl Pts',(20.7264713783391,18.4955827661252,19.3349614860924));
#191958=CARTESIAN_POINT('Ctrl Pts',(20.7057458574912,18.4385953023374,19.3385604267274));
#191959=CARTESIAN_POINT('Ctrl Pts',(20.6861858916074,18.3904136617868,19.3415464283923));
#191960=CARTESIAN_POINT('Ctrl Pts',(20.6401176740412,18.2879350372741,19.3478724572773));
#191961=CARTESIAN_POINT('Ctrl Pts',(20.613019857548,18.2339541350921,19.3511892495194));
#191962=CARTESIAN_POINT('Ctrl Pts',(20.5798101110025,18.1743050770372,19.3549125206352));
#191963=CARTESIAN_POINT('Ctrl Pts',(20.5759311443023,18.167428732909,19.3553426295591));
#191964=CARTESIAN_POINT('Ctrl Pts',(20.51786864747,18.0658321488365,19.361712715805));
#191965=CARTESIAN_POINT('Ctrl Pts',(20.4564797032099,17.9754193587445,19.3675896939138));
#191966=CARTESIAN_POINT('Ctrl Pts',(20.3413893847018,17.8312663816574,19.3778486639829));
#191967=CARTESIAN_POINT('Ctrl Pts',(20.2912758399324,17.7749443854973,19.3821204508981));
#191968=CARTESIAN_POINT('Ctrl Pts',(20.2250083159948,17.7080234638109,19.3876192747057));
#191969=CARTESIAN_POINT('Ctrl Pts',(20.2115679999666,17.6948083768271,19.388727274167));
#191970=CARTESIAN_POINT('Ctrl Pts',(20.1917686239179,17.6758540965962,19.3903500248149));
#191971=CARTESIAN_POINT('Ctrl Pts',(20.1855481252386,17.6699710118079,19.3908585250338));
#191972=CARTESIAN_POINT('Ctrl Pts',(20.1745788875875,17.6597221148441,19.3917529871309));
#191973=CARTESIAN_POINT('Ctrl Pts',(20.1698455343674,17.6553399444762,19.3921382405874));
#191974=CARTESIAN_POINT('Ctrl Pts',(20.1606152207652,17.6468724720768,19.3928881586286));
#191975=CARTESIAN_POINT('Ctrl Pts',(20.1561205516585,17.6427847574136,19.3932527150816));
#191976=CARTESIAN_POINT('Ctrl Pts',(20.1453330802512,17.6330585154702,19.3941262468744));
#191977=CARTESIAN_POINT('Ctrl Pts',(20.1390240312726,17.6274382360262,19.3946359832916));
#191978=CARTESIAN_POINT('Ctrl Pts',(20.1161325144858,17.6072903189353,19.3964814969577));
#191979=CARTESIAN_POINT('Ctrl Pts',(20.0993574525924,17.5929845496074,19.3978264252587));
#191980=CARTESIAN_POINT('Ctrl Pts',(19.9387768353313,17.4603170087698,19.4106353626249));
#191981=CARTESIAN_POINT('Ctrl Pts',(19.7801893562623,17.3611789023002,19.4229051906479));
#191982=CARTESIAN_POINT('Ctrl Pts',(19.5381685271012,17.2510619644581,19.4404589304331));
#191983=CARTESIAN_POINT('Ctrl Pts',(19.4637951469279,17.2221699746354,19.4456956537772));
#191984=CARTESIAN_POINT('Ctrl Pts',(19.3538073638813,17.1864463071912,19.4530667592979));
#191985=CARTESIAN_POINT('Ctrl Pts',(19.3193705705721,17.1762222545161,19.4553229664325));
#191986=CARTESIAN_POINT('Ctrl Pts',(19.2774855883302,17.1649384037487,19.4579916577795));
#191987=CARTESIAN_POINT('Ctrl Pts',(19.2702727999851,17.1630361018366,19.4584485389591));
#191988=CARTESIAN_POINT('Ctrl Pts',(19.259024140222,17.160132881136,19.4591567339893));
#191989=CARTESIAN_POINT('Ctrl Pts',(19.2549952027171,17.1591056834024,19.4594095256949));
#191990=CARTESIAN_POINT('Ctrl Pts',(19.2475051808882,17.157219547865,19.4598778440479));
#191991=CARTESIAN_POINT('Ctrl Pts',(19.2440449855488,17.1563574935375,19.4600935439111));
#191992=CARTESIAN_POINT('Ctrl Pts',(19.2362011946599,17.1544243699067,19.4605810457456));
#191993=CARTESIAN_POINT('Ctrl Pts',(19.2318163541602,17.1533585733641,19.46085254173));
#191994=CARTESIAN_POINT('Ctrl Pts',(19.2204825065344,17.1506420739839,19.4615517260124));
#191995=CARTESIAN_POINT('Ctrl Pts',(19.213528428697,17.1490124874761,19.4619782287922));
#191996=CARTESIAN_POINT('Ctrl Pts',(19.1706994361624,17.1392045263411,19.4645904096547));
#191997=CARTESIAN_POINT('Ctrl Pts',(19.1346222372207,17.1319268717651,19.4667279980098));
#191998=CARTESIAN_POINT('Ctrl Pts',(18.9307616996669,17.096307481435,19.4785481417348));
#191999=CARTESIAN_POINT('Ctrl Pts',(18.7602181564017,17.0873323709365,19.4875020295683));
#192000=CARTESIAN_POINT('Ctrl Pts',(18.49506777165,17.1053562507386,19.5021197903009));
#192001=CARTESIAN_POINT('Ctrl Pts',(18.4002683933502,17.1182878037721,19.5074782417262));
#192002=CARTESIAN_POINT('Ctrl Pts',(18.2857006414421,17.1418999000927,19.514289567983));
#192003=CARTESIAN_POINT('Ctrl Pts',(18.264795305158,17.1465401570512,19.5155460337669));
#192004=CARTESIAN_POINT('Ctrl Pts',(18.2351957923485,17.1535830257775,19.5173458105961));
#192005=CARTESIAN_POINT('Ctrl Pts',(18.2264406028694,17.1557253959756,19.5178807598492));
#192006=CARTESIAN_POINT('Ctrl Pts',(18.2113694560071,17.1595154357243,19.5188062072329));
#192007=CARTESIAN_POINT('Ctrl Pts',(18.2050468998075,17.1611365364247,19.5191958428496));
#192008=CARTESIAN_POINT('Ctrl Pts',(18.1929617117897,17.1642948085163,19.519943325187));
#192009=CARTESIAN_POINT('Ctrl Pts',(18.1871978726386,17.1658271460491,19.5203010119377));
#192010=CARTESIAN_POINT('Ctrl Pts',(18.172240217665,17.1698714438103,19.5212323636647));
#192011=CARTESIAN_POINT('Ctrl Pts',(18.163056828562,17.1724211503392,19.521807250392));
#192012=CARTESIAN_POINT('Ctrl Pts',(18.1318698905208,17.1813072563259,19.5237702288979));
#192013=CARTESIAN_POINT('Ctrl Pts',(18.1099526571315,17.1879384211769,19.525167880527));
#192014=CARTESIAN_POINT('Ctrl Pts',(17.9198016564213,17.2488534802855,19.5374567847258));
#192015=CARTESIAN_POINT('Ctrl Pts',(17.7589032007386,17.3236473035647,19.54906343178));
#192016=CARTESIAN_POINT('Ctrl Pts',(17.5362478090133,17.4632887554085,19.5664272026954));
#192017=CARTESIAN_POINT('Ctrl Pts',(17.4661479045323,17.513455342853,19.5721005278551));
#192018=CARTESIAN_POINT('Ctrl Pts',(17.3701133608509,17.5914582036778,19.5799980769635));
#192019=CARTESIAN_POINT('Ctrl Pts',(17.3415659197429,17.6159356972641,19.582362553619));
#192020=CARTESIAN_POINT('Ctrl Pts',(17.308078630144,17.6462334421172,19.5851413824312));
#192021=CARTESIAN_POINT('Ctrl Pts',(17.3025006758277,17.651334708172,19.585604426057));
#192022=CARTESIAN_POINT('Ctrl Pts',(17.2938810828393,17.6593028736466,19.5863200711913));
#192023=CARTESIAN_POINT('Ctrl Pts',(17.2908204753074,17.6621490298603,19.5865742001909));
#192024=CARTESIAN_POINT('Ctrl Pts',(17.2851656038936,17.6674389890509,19.5870437409577));
#192025=CARTESIAN_POINT('Ctrl Pts',(17.2825691051605,17.6698802578435,19.5872593338399));
#192026=CARTESIAN_POINT('Ctrl Pts',(17.2767199459259,17.6754076234548,19.5877450095963));
#192027=CARTESIAN_POINT('Ctrl Pts',(17.2734709263437,17.6784974946967,19.5880147962159));
#192028=CARTESIAN_POINT('Ctrl Pts',(17.2639304848178,17.687628509944,19.5888071153665));
#192029=CARTESIAN_POINT('Ctrl Pts',(17.2576664645815,17.6936983245562,19.5893274822458));
#192030=CARTESIAN_POINT('Ctrl Pts',(17.2133360265989,17.7371888149357,19.5930127586802));
#192031=CARTESIAN_POINT('Ctrl Pts',(17.1766560206251,17.7760020625543,19.5960761603608));
#192032=CARTESIAN_POINT('Ctrl Pts',(17.132465941483,17.8264550157788,19.5998478811659));
#192033=CARTESIAN_POINT('Ctrl Pts',(17.1235520946257,17.8368334491352,19.6006131075048));
#192034=CARTESIAN_POINT('Ctrl Pts',(17.0811101336374,17.8872290511397,19.604282006823));
#192035=CARTESIAN_POINT('Ctrl Pts',(17.0489682802044,17.9283921402587,19.6071384933003));
#192036=CARTESIAN_POINT('Ctrl Pts',(16.9542697452041,18.0593822573851,19.615939036211));
#192037=CARTESIAN_POINT('Ctrl Pts',(16.8971322488468,18.1528983059434,19.6218308921262));
#192038=CARTESIAN_POINT('Ctrl Pts',(16.813078747798,18.3179720091444,19.6321302032128));
#192039=CARTESIAN_POINT('Ctrl Pts',(16.7823335285292,18.3873291412583,19.636427835384));
#192040=CARTESIAN_POINT('Ctrl Pts',(16.7486505848235,18.4758575711171,19.6419578096697));
#192041=CARTESIAN_POINT('Ctrl Pts',(16.7421624441066,18.493622966858,19.6430695301577));
#192042=CARTESIAN_POINT('Ctrl Pts',(16.7330803287254,18.5195645535797,19.644696740902));
#192043=CARTESIAN_POINT('Ctrl Pts',(16.7302965253457,18.5276736578911,19.6452059309915));
#192044=CARTESIAN_POINT('Ctrl Pts',(16.725504182462,18.5419146669503,19.6461011909323));
#192045=CARTESIAN_POINT('Ctrl Pts',(16.7234742631139,18.5480392984,19.6464865484062));
#192046=CARTESIAN_POINT('Ctrl Pts',(16.7195884541046,18.5599454756006,19.6472363604058));
#192047=CARTESIAN_POINT('Ctrl Pts',(16.7177293756122,18.5657259202373,19.6476007053494));
#192048=CARTESIAN_POINT('Ctrl Pts',(16.7133468280937,18.5795564707534,19.6484732322496));
#192049=CARTESIAN_POINT('Ctrl Pts',(16.7108465750286,18.587613773359,19.6489821713322));
#192050=CARTESIAN_POINT('Ctrl Pts',(16.7020108021116,18.6167010056546,19.6508218523817));
#192051=CARTESIAN_POINT('Ctrl Pts',(16.6959546563562,18.6378137168152,19.6521616702444));
#192052=CARTESIAN_POINT('Ctrl Pts',(16.6414577136117,18.8395937628833,19.6650134957142));
#192053=CARTESIAN_POINT('Ctrl Pts',(16.6168436525267,19.0258066914941,19.6773392599676));
#192054=CARTESIAN_POINT('Ctrl Pts',(16.6170536900505,19.2757905700977,19.6938412690976));
#192055=CARTESIAN_POINT('Ctrl Pts',(16.6199199093842,19.3387716912197,19.6979837650249));
#192056=CARTESIAN_POINT('Ctrl Pts',(16.6300811408575,19.4512138925938,19.7052635137628));
#192057=CARTESIAN_POINT('Ctrl Pts',(16.6363255963833,19.5007244264126,19.7084278687014));
#192058=CARTESIAN_POINT('Ctrl Pts',(16.6455655237812,19.5576864818788,19.711986617993));
#192059=CARTESIAN_POINT('Ctrl Pts',(16.6468596259024,19.5653940480585,19.7124664019341));
#192060=CARTESIAN_POINT('Ctrl Pts',(16.6489941842195,19.5776899281943,19.7132288084176));
#192061=CARTESIAN_POINT('Ctrl Pts',(16.6498071586511,19.5822828521593,19.713512924633));
#192062=CARTESIAN_POINT('Ctrl Pts',(16.6512728103081,19.5904065696733,19.7140142252334));
#192063=CARTESIAN_POINT('Ctrl Pts',(16.6519192986531,19.5939384357997,19.714231757366));
#192064=CARTESIAN_POINT('Ctrl Pts',(16.6533073565621,19.6014141734707,19.7146913079822));
#192065=CARTESIAN_POINT('Ctrl Pts',(16.6540511534524,19.60535757843,19.7149331980395));
#192066=CARTESIAN_POINT('Ctrl Pts',(16.6560859627934,19.6159796595447,19.7155834164187));
#192067=CARTESIAN_POINT('Ctrl Pts',(16.6573979718346,19.6226543333368,19.7159905648095));
#192068=CARTESIAN_POINT('Ctrl Pts',(16.6640292674551,19.6555515422671,19.7179906964502));
#192069=CARTESIAN_POINT('Ctrl Pts',(16.6698134445377,19.6816792138249,19.7195586405791));
#192070=CARTESIAN_POINT('Ctrl Pts',(16.6879077566179,19.756648145912,19.7240162630924));
#192071=CARTESIAN_POINT('Ctrl Pts',(16.7014678348523,19.8051708858565,19.7268505491724));
#192072=CARTESIAN_POINT('Ctrl Pts',(16.7257202826567,19.881355665803,19.731284302869));
#192073=CARTESIAN_POINT('Ctrl Pts',(16.735280380112,19.9093428335651,19.73290946559));
#192074=CARTESIAN_POINT('Ctrl Pts',(16.7454193946088,19.9371103055747,19.7345260524097));
#192075=CARTESIAN_POINT('Origin',(18.734,19.211,0.));
#192076=CARTESIAN_POINT('',(16.7454193572566,19.9371102032791,20.755413683557));
#192077=CARTESIAN_POINT('',(16.7454193623258,19.9371102171621,20.5336910458214));
#192078=CARTESIAN_POINT('',(16.7454193623258,19.9371102171621,0.));
#192079=CARTESIAN_POINT('Ctrl Pts',(16.7454193572565,19.9371102032791,20.755413683557));
#192080=CARTESIAN_POINT('Ctrl Pts',(16.7360405234064,19.9114246153868,20.7536067709888));
#192081=CARTESIAN_POINT('Ctrl Pts',(16.7271552312975,19.8855460612012,20.7517981507751));
#192082=CARTESIAN_POINT('Ctrl Pts',(16.6954799915782,19.7871126977697,20.7449759971118));
#192083=CARTESIAN_POINT('Ctrl Pts',(16.6761041950082,19.7135297019902,20.7399903579701));
#192084=CARTESIAN_POINT('Ctrl Pts',(16.6536719560301,19.6048809317995,20.7329253866806));
#192085=CARTESIAN_POINT('Ctrl Pts',(16.6474610431052,19.5705309000379,20.7307344299769));
#192086=CARTESIAN_POINT('Ctrl Pts',(16.640966352227,19.5287323593999,20.7281324028596));
#192087=CARTESIAN_POINT('Ctrl Pts',(16.6398690489289,19.5214178899481,20.7276794301417));
#192088=CARTESIAN_POINT('Ctrl Pts',(16.638216799776,19.5099965700239,20.7269759736824));
#192089=CARTESIAN_POINT('Ctrl Pts',(16.6376355527492,19.5058936693283,20.7267240430256));
#192090=CARTESIAN_POINT('Ctrl Pts',(16.6365763773633,19.4982557595705,20.7262565239903));
#192091=CARTESIAN_POINT('Ctrl Pts',(16.6360953412418,19.4947212844061,20.7260407673694));
#192092=CARTESIAN_POINT('Ctrl Pts',(16.6350235901553,19.4866946828845,20.7255521198264));
#192093=CARTESIAN_POINT('Ctrl Pts',(16.6344383623656,19.4822018766634,20.725279541175));
#192094=CARTESIAN_POINT('Ctrl Pts',(16.6327408111968,19.4688348488033,20.7244712559344));
#192095=CARTESIAN_POINT('Ctrl Pts',(16.6316702786934,19.4599552913088,20.7239378480796));
#192096=CARTESIAN_POINT('Ctrl Pts',(16.6239226573551,19.3920751822681,20.7198852923423));
#192097=CARTESIAN_POINT('Ctrl Pts',(16.6196735634268,19.3328182834744,20.716492044051));
#192098=CARTESIAN_POINT('Ctrl Pts',(16.617322962857,19.2531770715579,20.7120327766097));
#192099=CARTESIAN_POINT('Ctrl Pts',(16.617015959299,19.2328903772815,20.7109057039679));
#192100=CARTESIAN_POINT('Ctrl Pts',(16.6168948154794,19.0728053060273,20.7020607908922));
#192101=CARTESIAN_POINT('Ctrl Pts',(16.6306360838822,18.9333414187302,20.6946257313364));
#192102=CARTESIAN_POINT('Ctrl Pts',(16.67575019094,18.7075305319075,20.681879489083));
#192103=CARTESIAN_POINT('Ctrl Pts',(16.6991411766927,18.6200512110003,20.6767637970216));
#192104=CARTESIAN_POINT('Ctrl Pts',(16.7324403978102,18.521335896224,20.6706560331205));
#192105=CARTESIAN_POINT('Ctrl Pts',(16.7369541254703,18.5083726599828,20.6698472613802));
#192106=CARTESIAN_POINT('Ctrl Pts',(16.7443954423061,18.4876526260788,20.6685433693409));
#192107=CARTESIAN_POINT('Ctrl Pts',(16.747243134023,18.4798674047311,20.6680509030762));
#192108=CARTESIAN_POINT('Ctrl Pts',(16.7523808176238,18.4660733160688,20.6671737171445));
#192109=CARTESIAN_POINT('Ctrl Pts',(16.7546526122558,18.4600577481487,20.6667896098438));
#192110=CARTESIAN_POINT('Ctrl Pts',(16.759443379556,18.4475448853049,20.6659873210957));
#192111=CARTESIAN_POINT('Ctrl Pts',(16.7619670934187,18.4410494996128,20.6655689840444));
#192112=CARTESIAN_POINT('Ctrl Pts',(16.7686050585362,18.4242118372076,20.6644796217732));
#192113=CARTESIAN_POINT('Ctrl Pts',(16.7727688479728,18.4138894368112,20.6638069323112));
#192114=CARTESIAN_POINT('Ctrl Pts',(16.7912114314484,18.3691880444909,20.660872359401));
#192115=CARTESIAN_POINT('Ctrl Pts',(16.8063135236491,18.3351579117907,20.6585826975868));
#192116=CARTESIAN_POINT('Ctrl Pts',(16.8488257062101,18.2457962822775,20.6524166966283));
#192117=CARTESIAN_POINT('Ctrl Pts',(16.8777709759424,18.1912387444737,20.6484905850074));
#192118=CARTESIAN_POINT('Ctrl Pts',(16.983280513165,18.0117849697807,20.6350415605223));
#192119=CARTESIAN_POINT('Ctrl Pts',(17.0704029012234,17.8935878040075,20.625236349674));
#192120=CARTESIAN_POINT('Ctrl Pts',(17.1821607821435,17.770907906973,20.6144037596385));
#192121=CARTESIAN_POINT('Ctrl Pts',(17.195508363814,17.7566569480662,20.6131348281491));
#192122=CARTESIAN_POINT('Ctrl Pts',(17.2456831712661,17.7045501633054,20.6084613457109));
#192123=CARTESIAN_POINT('Ctrl Pts',(17.2837290690397,17.6678884260932,20.6051051910233));
#192124=CARTESIAN_POINT('Ctrl Pts',(17.3295906258319,17.6268917727283,20.6013107135223));
#192125=CARTESIAN_POINT('Ctrl Pts',(17.3361072842789,17.6211382049882,20.600777191963));
#192126=CARTESIAN_POINT('Ctrl Pts',(17.3460336042793,17.6124824593865,20.599973286667));
#192127=CARTESIAN_POINT('Ctrl Pts',(17.3494172446117,17.6095507695739,20.5997007814424));
#192128=CARTESIAN_POINT('Ctrl Pts',(17.3555106504386,17.6043050039595,20.599212817212));
#192129=CARTESIAN_POINT('Ctrl Pts',(17.3582169678206,17.6019870273679,20.5989970721733));
#192130=CARTESIAN_POINT('Ctrl Pts',(17.3641139118961,17.5969620162716,20.5985291006686));
#192131=CARTESIAN_POINT('Ctrl Pts',(17.3673067049495,17.5942576132054,20.5982770668745));
#192132=CARTESIAN_POINT('Ctrl Pts',(17.3763062272574,17.5866804253261,20.5975703516761));
#192133=CARTESIAN_POINT('Ctrl Pts',(17.3821312080661,17.5818292801102,20.5971172261746));
#192134=CARTESIAN_POINT('Ctrl Pts',(17.4172901011271,17.552866753344,20.5944070627941));
#192135=CARTESIAN_POINT('Ctrl Pts',(17.4472443095138,17.5295152340343,20.5922013604281));
#192136=CARTESIAN_POINT('Ctrl Pts',(17.5483211305015,17.4550023281803,20.5850329287542));
#192137=CARTESIAN_POINT('Ctrl Pts',(17.621993752691,17.4074460801967,20.5802384872086));
#192138=CARTESIAN_POINT('Ctrl Pts',(17.8507219828837,17.2791596527319,20.5659712393524));
#192139=CARTESIAN_POINT('Ctrl Pts',(18.013003440267,17.212914815332,20.5565783590459));
#192140=CARTESIAN_POINT('Ctrl Pts',(18.2038288681461,17.1613319378261,20.5450925151874));
#192141=CARTESIAN_POINT('Ctrl Pts',(18.2261824781215,17.1556796120311,20.5437418037939));
#192142=CARTESIAN_POINT('Ctrl Pts',(18.2579259575103,17.1482024222837,20.5418145608796));
#192143=CARTESIAN_POINT('Ctrl Pts',(18.2672432067356,17.1460742308853,20.5412477787274));
#192144=CARTESIAN_POINT('Ctrl Pts',(18.2824025517023,17.1427194641068,20.5403237036973));
#192145=CARTESIAN_POINT('Ctrl Pts',(18.2882360530709,17.1414543655773,20.5399676506763));
#192146=CARTESIAN_POINT('Ctrl Pts',(18.3004557869014,17.1388583614571,20.5392208176931));
#192147=CARTESIAN_POINT('Ctrl Pts',(18.3068429680259,17.1375322709405,20.5388298878124));
#192148=CARTESIAN_POINT('Ctrl Pts',(18.3220482928485,17.1344486187132,20.5378978528599));
#192149=CARTESIAN_POINT('Ctrl Pts',(18.3308716521666,17.1327176853411,20.5373559034082));
#192150=CARTESIAN_POINT('Ctrl Pts',(18.3606150748435,17.1270792691438,20.5355251291983));
#192151=CARTESIAN_POINT('Ctrl Pts',(18.3815824373881,17.1234311449693,20.5342280935267));
#192152=CARTESIAN_POINT('Ctrl Pts',(18.5599586830884,17.0951592204248,20.5231357202773));
#192153=CARTESIAN_POINT('Ctrl Pts',(18.7196001142215,17.0880664030753,20.512767393336));
#192154=CARTESIAN_POINT('Ctrl Pts',(19.0098595657144,17.1079241099886,20.4935492169254));
#192155=CARTESIAN_POINT('Ctrl Pts',(19.1401117332352,17.1291484027072,20.484806486761));
#192156=CARTESIAN_POINT('Ctrl Pts',(19.2827906698167,17.1663079376869,20.4756083278399));
#192157=CARTESIAN_POINT('Ctrl Pts',(19.2979808493031,17.1704455498151,20.4746342580374));
#192158=CARTESIAN_POINT('Ctrl Pts',(19.3187013255591,17.1763386072796,20.4733140308221));
#192159=CARTESIAN_POINT('Ctrl Pts',(19.3242722228199,17.1779477803255,20.4729599180036));
#192160=CARTESIAN_POINT('Ctrl Pts',(19.3331114559787,17.1805404187054,20.4723994731689));
#192161=CARTESIAN_POINT('Ctrl Pts',(19.3363840983638,17.181508919365,20.4721922835853));
#192162=CARTESIAN_POINT('Ctrl Pts',(19.343135687307,17.1835247439,20.4717655043878));
#192163=CARTESIAN_POINT('Ctrl Pts',(19.3466142814251,17.1845731096357,20.4715459830207));
#192164=CARTESIAN_POINT('Ctrl Pts',(19.3548927620743,17.1870913120957,20.4710243987543));
#192165=CARTESIAN_POINT('Ctrl Pts',(19.3596901894528,17.1885692874724,20.4707228105293));
#192166=CARTESIAN_POINT('Ctrl Pts',(19.3758346181164,17.1936059533133,20.4697100255666));
#192167=CARTESIAN_POINT('Ctrl Pts',(19.3871571164829,17.1972432588737,20.4690032816683));
#192168=CARTESIAN_POINT('Ctrl Pts',(19.5222534827858,17.2419017272187,20.4606065190369));
#192169=CARTESIAN_POINT('Ctrl Pts',(19.6420314235768,17.2941848349504,20.4535133207687));
#192170=CARTESIAN_POINT('Ctrl Pts',(19.8982625207909,17.435476969937,20.4376172869786));
#192171=CARTESIAN_POINT('Ctrl Pts',(20.0307900535159,17.529834386761,20.428838921153));
#192172=CARTESIAN_POINT('Ctrl Pts',(20.1688705616499,17.6542731541333,20.4180456363176));
#192173=CARTESIAN_POINT('Ctrl Pts',(20.1862277694474,17.6704525518004,20.4166562195909));
#192174=CARTESIAN_POINT('Ctrl Pts',(20.2102693970498,17.6936301882928,20.4146831158096));
#192175=CARTESIAN_POINT('Ctrl Pts',(20.2171837810385,17.700388089184,20.4141098265459));
#192176=CARTESIAN_POINT('Ctrl Pts',(20.228305950999,17.7114085239148,20.4131780419522));
#192177=CARTESIAN_POINT('Ctrl Pts',(20.2325424151096,17.7156420163315,20.4128208286025));
#192178=CARTESIAN_POINT('Ctrl Pts',(20.2413434535371,17.7245118420871,20.412073895761));
#192179=CARTESIAN_POINT('Ctrl Pts',(20.2459047272847,17.729151348928,20.4116840366554));
#192180=CARTESIAN_POINT('Ctrl Pts',(20.2566525961092,17.7401848423212,20.4107588149818));
#192181=CARTESIAN_POINT('Ctrl Pts',(20.2628203769044,17.746596910724,20.4102226404731));
#192182=CARTESIAN_POINT('Ctrl Pts',(20.283224528661,17.7680786142498,20.4084312197407));
#192183=CARTESIAN_POINT('Ctrl Pts',(20.2972795993635,17.7833180984901,20.4071682347395));
#192184=CARTESIAN_POINT('Ctrl Pts',(20.3711079567019,17.8657654173804,20.4003747605943));
#192185=CARTESIAN_POINT('Ctrl Pts',(20.4267690679071,17.9365166427092,20.3946763524443));
#192186=CARTESIAN_POINT('Ctrl Pts',(20.5545411153404,18.1221220128579,20.3800734122205));
#192187=CARTESIAN_POINT('Ctrl Pts',(20.6204437707324,18.240767324393,20.371023215521));
#192188=CARTESIAN_POINT('Ctrl Pts',(20.7047480655799,18.4341176291726,20.3572297754403));
#192189=CARTESIAN_POINT('Ctrl Pts',(20.7312131745221,18.5049290342137,20.3523672098846));
#192190=CARTESIAN_POINT('Ctrl Pts',(20.7566811408368,18.5860679108787,20.3471148050684));
#192191=CARTESIAN_POINT('Ctrl Pts',(20.7594631137464,18.5951442570876,20.3465316864768));
#192192=CARTESIAN_POINT('Ctrl Pts',(20.7634966847071,18.6086270399203,20.3456723383378));
#192193=CARTESIAN_POINT('Ctrl Pts',(20.7647951422279,18.6130191746498,20.3453934740385));
#192194=CARTESIAN_POINT('Ctrl Pts',(20.7670808066898,18.6208439272097,20.3448986234403));
#192195=CARTESIAN_POINT('Ctrl Pts',(20.7680735885011,18.6242748565138,20.344682315733));
#192196=CARTESIAN_POINT('Ctrl Pts',(20.770190244178,18.6316596982541,20.3442181766255));
#192197=CARTESIAN_POINT('Ctrl Pts',(20.7713112837345,18.6356143644983,20.3439705109225));
#192198=CARTESIAN_POINT('Ctrl Pts',(20.7743759483835,18.6465467646867,20.3432882379141));
#192199=CARTESIAN_POINT('Ctrl Pts',(20.7762953124382,18.6535313229972,20.3428550183408));
#192200=CARTESIAN_POINT('Ctrl Pts',(20.7866460997443,18.6919688314418,20.3404849055409));
#192201=CARTESIAN_POINT('Ctrl Pts',(20.7943873030811,18.723605099902,20.3385855181239));
#192202=CARTESIAN_POINT('Ctrl Pts',(20.8364003226817,18.9142532930349,20.3273768860303));
#192203=CARTESIAN_POINT('Ctrl Pts',(20.8529854148541,19.0766185712416,20.3187795159991));
#192204=CARTESIAN_POINT('Ctrl Pts',(20.8492493029358,19.3561189756619,20.3034769374846));
#192205=CARTESIAN_POINT('Ctrl Pts',(20.8380201751821,19.4725969651671,20.2969546458735));
#192206=CARTESIAN_POINT('Ctrl Pts',(20.8147015453552,19.6016075761323,20.2892743087989));
#192207=CARTESIAN_POINT('Ctrl Pts',(20.8120175823736,19.6156431907405,20.2884328051853));
#192208=CARTESIAN_POINT('Ctrl Pts',(20.8075198239715,19.6379379582523,20.2870862350652));
#192209=CARTESIAN_POINT('Ctrl Pts',(20.8057982552639,19.6462154258775,20.2865841097929));
#192210=CARTESIAN_POINT('Ctrl Pts',(20.8026745717422,19.6607957376827,20.2856957086019));
#192211=CARTESIAN_POINT('Ctrl Pts',(20.8012931104012,19.6671029310064,20.285310098715));
#192212=CARTESIAN_POINT('Ctrl Pts',(20.7983761289868,19.6801351416822,20.2845105958341));
#192213=CARTESIAN_POINT('Ctrl Pts',(20.7968365513906,19.686859163605,20.2840965764881));
#192214=CARTESIAN_POINT('Ctrl Pts',(20.7928002866257,19.7040995917253,20.2830310859916));
#192215=CARTESIAN_POINT('Ctrl Pts',(20.7902558947911,19.7146045233325,20.2823780853774));
#192216=CARTESIAN_POINT('Ctrl Pts',(20.7793002306081,19.7583690818196,20.2796415347955));
#192217=CARTESIAN_POINT('Ctrl Pts',(20.7701619401166,19.791439731883,20.2775346424721));
#192218=CARTESIAN_POINT('Ctrl Pts',(20.7442602346618,19.8770178220103,20.271976989016));
#192219=CARTESIAN_POINT('Ctrl Pts',(20.7262436205413,19.9291159277158,20.2684877867773));
#192220=CARTESIAN_POINT('Ctrl Pts',(20.6664544650889,20.0823648364326,20.2579141975199));
#192221=CARTESIAN_POINT('Ctrl Pts',(20.6188549990231,20.1810387129481,20.2506814311898));
#192222=CARTESIAN_POINT('Ctrl Pts',(20.5395024012637,20.3174330896548,20.2402577092099));
#192223=CARTESIAN_POINT('Ctrl Pts',(20.5137261904854,20.3584354126835,20.2370658065293));
#192224=CARTESIAN_POINT('Ctrl Pts',(20.4766412853106,20.4131661283792,20.2327528104882));
#192225=CARTESIAN_POINT('Ctrl Pts',(20.466532949448,20.4276888070272,20.2316031723067));
#192226=CARTESIAN_POINT('Ctrl Pts',(20.4252231428441,20.4854798161267,20.2270120691498));
#192227=CARTESIAN_POINT('Ctrl Pts',(20.392570622119,20.527692465452,20.2236210422723));
#192228=CARTESIAN_POINT('Ctrl Pts',(20.3527633195014,20.575320471957,20.2197919159971));
#192229=CARTESIAN_POINT('Ctrl Pts',(20.347129931257,20.5819766101782,20.2192567223926));
#192230=CARTESIAN_POINT('Ctrl Pts',(20.3385381903742,20.5920019165778,20.2184507840164));
#192231=CARTESIAN_POINT('Ctrl Pts',(20.3356100771738,20.5953967131972,20.2181779024872));
#192232=CARTESIAN_POINT('Ctrl Pts',(20.3303348968112,20.6014735159223,20.2176895258111));
#192233=CARTESIAN_POINT('Ctrl Pts',(20.3279918318567,20.6041589075969,20.2174737425564));
#192234=CARTESIAN_POINT('Ctrl Pts',(20.3228860001873,20.6099809681146,20.2170059934483));
#192235=CARTESIAN_POINT('Ctrl Pts',(20.3201207309398,20.6131153655511,20.216754218622));
#192236=CARTESIAN_POINT('Ctrl Pts',(20.3123276496866,20.6218961655882,20.2160489478122));
#192237=CARTESIAN_POINT('Ctrl Pts',(20.3072787890959,20.6275239198566,20.2155969976132));
#192238=CARTESIAN_POINT('Ctrl Pts',(20.2769247814778,20.6609957750554,20.2129085161081));
#192239=CARTESIAN_POINT('Ctrl Pts',(20.250909449883,20.6881901513942,20.210722371243));
#192240=CARTESIAN_POINT('Ctrl Pts',(20.1629330384616,20.775376880385,20.2036492250293));
#192241=CARTESIAN_POINT('Ctrl Pts',(20.0980283284796,20.8322815061929,20.1989254518203));
#192242=CARTESIAN_POINT('Ctrl Pts',(19.8901866664579,20.9931630123345,20.1846219515936));
#192243=CARTESIAN_POINT('Ctrl Pts',(19.7375871759269,21.0833457862731,20.1751335931527));
#192244=CARTESIAN_POINT('Ctrl Pts',(19.5545465211021,21.1626447596673,20.1635411669508));
#192245=CARTESIAN_POINT('Ctrl Pts',(19.5333788633068,21.1714099657586,20.1621989074792));
#192246=CARTESIAN_POINT('Ctrl Pts',(19.5032080725475,21.1833333431225,20.1602816822511));
#192247=CARTESIAN_POINT('Ctrl Pts',(19.4943189799726,21.1867770419358,20.1597163275187));
#192248=CARTESIAN_POINT('Ctrl Pts',(19.4798309069186,21.1922775760549,20.1587939581265));
#192249=CARTESIAN_POINT('Ctrl Pts',(19.4742458956537,21.1943710162095,20.1584381742932));
#192250=CARTESIAN_POINT('Ctrl Pts',(19.4625309178412,21.1987057884483,20.1576913988496));
#192251=CARTESIAN_POINT('Ctrl Pts',(19.4563992920302,21.2009424265729,20.1573002550875));
#192252=CARTESIAN_POINT('Ctrl Pts',(19.4417770756449,21.2061996955185,20.1563667729603));
#192253=CARTESIAN_POINT('Ctrl Pts',(19.4332773991719,21.20919451728,20.1558235830666));
#192254=CARTESIAN_POINT('Ctrl Pts',(19.4045268851145,21.2191187231953,20.1539841510221));
#192255=CARTESIAN_POINT('Ctrl Pts',(19.3841906717087,21.2257950634593,20.1526795911252));
#192256=CARTESIAN_POINT('Ctrl Pts',(19.2725841393161,21.2605696324252,20.1454989502379));
#192257=CARTESIAN_POINT('Ctrl Pts',(19.1796055673667,21.2827721807551,20.1394327631581));
#192258=CARTESIAN_POINT('Ctrl Pts',(18.9174387483159,21.3269086169007,20.1221549648676));
#192259=CARTESIAN_POINT('Ctrl Pts',(18.7466315512495,21.3348070588791,20.1106593089952));
#192260=CARTESIAN_POINT('Ctrl Pts',(18.540137215944,21.3194242056132,20.0974444597342));
#192261=CARTESIAN_POINT('Ctrl Pts',(18.5036195834844,21.3157471696094,20.0951364750847));
#192262=CARTESIAN_POINT('Ctrl Pts',(18.4601344208153,21.3102230867747,20.0924371611454));
#192263=CARTESIAN_POINT('Ctrl Pts',(18.4530597181988,21.3092879890239,20.09199956308));
#192264=CARTESIAN_POINT('Ctrl Pts',(18.4415211199964,21.3077034721454,20.0912885523864));
#192265=CARTESIAN_POINT('Ctrl Pts',(18.4370543994273,21.3070755369323,20.0910139727803));
#192266=CARTESIAN_POINT('Ctrl Pts',(18.4290601394359,21.3059256303732,20.0905237723634));
#192267=CARTESIAN_POINT('Ctrl Pts',(18.4255318936259,21.3054090200606,20.0903078539851));
#192268=CARTESIAN_POINT('Ctrl Pts',(18.4178911011047,21.3042705183525,20.0898411977077));
#192269=CARTESIAN_POINT('Ctrl Pts',(18.4137790897344,21.3036454234477,20.0895906433677));
#192270=CARTESIAN_POINT('Ctrl Pts',(18.4022912549831,21.3018644256533,20.0888922292462));
#192271=CARTESIAN_POINT('Ctrl Pts',(18.3949195806381,21.3006816051628,20.0884458673054));
#192272=CARTESIAN_POINT('Ctrl Pts',(18.3520181323961,21.2935648644531,20.0858578672664));
#192273=CARTESIAN_POINT('Ctrl Pts',(18.3166358985153,21.2867635022141,20.0837623328045));
#192274=CARTESIAN_POINT('Ctrl Pts',(18.2031781593225,21.2619353364722,20.0771188420649));
#192275=CARTESIAN_POINT('Ctrl Pts',(18.1259430232486,21.2403783037761,20.0727122632516));
#192276=CARTESIAN_POINT('Ctrl Pts',(17.8744321063013,21.1545254361515,20.0582244897316));
#192277=CARTESIAN_POINT('Ctrl Pts',(17.7074238363211,21.0717212179973,20.0482960852484));
#192278=CARTESIAN_POINT('Ctrl Pts',(17.5350110583752,20.9558790549349,20.0362152447816));
#192279=CARTESIAN_POINT('Ctrl Pts',(17.5168619472329,20.9432679656353,20.0349197419333));
#192280=CARTESIAN_POINT('Ctrl Pts',(17.4920448525922,20.9254410011361,20.0331134932818));
#192281=CARTESIAN_POINT('Ctrl Pts',(17.4852053367591,20.9204655364926,20.0326119737449));
#192282=CARTESIAN_POINT('Ctrl Pts',(17.4735025671535,20.9118445433144,20.0317473342323));
#192283=CARTESIAN_POINT('Ctrl Pts',(17.4686248260444,20.9082187857452,20.0313849848891));
#192284=CARTESIAN_POINT('Ctrl Pts',(17.4587692539056,20.9008267684271,20.0306488192116));
#192285=CARTESIAN_POINT('Ctrl Pts',(17.4537923346029,20.8970593984915,20.0302749615523));
#192286=CARTESIAN_POINT('Ctrl Pts',(17.4422650104339,20.8882531158872,20.0294041018187));
#192287=CARTESIAN_POINT('Ctrl Pts',(17.4357273382998,20.8831977726572,20.028906453325));
#192288=CARTESIAN_POINT('Ctrl Pts',(17.4220467693018,20.8724905006463,20.0278571079414));
#192289=CARTESIAN_POINT('Ctrl Pts',(17.4149104277188,20.8668305044623,20.0273050948379));
#192290=CARTESIAN_POINT('Ctrl Pts',(17.3960102361514,20.8516406053842,20.0258306232565));
#192291=CARTESIAN_POINT('Ctrl Pts',(17.3843118766357,20.8420303967656,20.0249049528496));
#192292=CARTESIAN_POINT('Ctrl Pts',(17.3489534044081,20.812342501638,20.0220665889949));
#192293=CARTESIAN_POINT('Ctrl Pts',(17.3256315849277,20.791870054702,20.0201380780432));
#192294=CARTESIAN_POINT('Ctrl Pts',(17.1786346376612,20.6569976316224,20.0076111770037));
#192295=CARTESIAN_POINT('Ctrl Pts',(17.0685545541891,20.528704513821,19.9964228356037));
#192296=CARTESIAN_POINT('Ctrl Pts',(16.9197639325812,20.3064650164272,19.9788045468916));
#192297=CARTESIAN_POINT('Ctrl Pts',(16.8705050518759,20.2203994973653,19.9723517881039));
#192298=CARTESIAN_POINT('Ctrl Pts',(16.823235326096,20.1224611060637,19.9656327721567));
#192299=CARTESIAN_POINT('Ctrl Pts',(16.8190812888893,20.1137011271451,19.965037099068));
#192300=CARTESIAN_POINT('Ctrl Pts',(16.8130369086222,20.1007253175875,19.9641628924462));
#192301=CARTESIAN_POINT('Ctrl Pts',(16.8111000205983,20.0965314841057,19.9638815930442));
#192302=CARTESIAN_POINT('Ctrl Pts',(16.8076882729761,20.0890802443734,19.9633840592414));
#192303=CARTESIAN_POINT('Ctrl Pts',(16.8062079245864,20.0858254110856,19.9631674899564));
#192304=CARTESIAN_POINT('Ctrl Pts',(16.8030539888957,20.0788439893014,19.9627046029928));
#192305=CARTESIAN_POINT('Ctrl Pts',(16.8013829439056,20.0751163131825,19.9624584414997));
#192306=CARTESIAN_POINT('Ctrl Pts',(16.7968258155018,20.0648711758014,19.9617845528517));
#192307=CARTESIAN_POINT('Ctrl Pts',(16.7939618108712,20.0583438699625,19.9613581576325));
#192308=CARTESIAN_POINT('Ctrl Pts',(16.7788510569385,20.023426951888,19.9590922720175));
#192309=CARTESIAN_POINT('Ctrl Pts',(16.7671936889874,19.9947844752305,19.9572865043125));
#192310=CARTESIAN_POINT('Ctrl Pts',(16.7525148722082,19.9563258362801,19.9549187002088));
#192311=CARTESIAN_POINT('Ctrl Pts',(16.7489321373149,19.9467305698026,19.9543325877505));
#192312=CARTESIAN_POINT('Ctrl Pts',(16.7454193617555,19.9371102156003,19.9537492222746));
#192313=CARTESIAN_POINT('',(16.6170003908425,19.209713599163,20.489056279057));
#192314=CARTESIAN_POINT('Ctrl Pts',(16.7454193946088,19.9371103055747,19.7345260524097));
#192315=CARTESIAN_POINT('Ctrl Pts',(16.7805470626998,20.0333135944443,19.7401268852385));
#192316=CARTESIAN_POINT('Ctrl Pts',(16.8226235252127,20.1268794616034,19.745631482775));
#192317=CARTESIAN_POINT('Ctrl Pts',(16.9207547019587,20.3085630814941,19.7569906986618));
#192318=CARTESIAN_POINT('Ctrl Pts',(16.9768430326951,20.3962841744325,19.7628328189229));
#192319=CARTESIAN_POINT('Ctrl Pts',(17.0475681360481,20.4907789738437,19.769749572138));
#192320=CARTESIAN_POINT('Ctrl Pts',(17.0561041186966,20.501950057493,19.7705776639458));
#192321=CARTESIAN_POINT('Ctrl Pts',(17.0699092553026,20.5196486712185,19.7719067762762));
#192322=CARTESIAN_POINT('Ctrl Pts',(17.0751071271934,20.5262314567147,19.7724049751719));
#192323=CARTESIAN_POINT('Ctrl Pts',(17.0843685901543,20.5378182854468,19.7732888190482));
#192324=CARTESIAN_POINT('Ctrl Pts',(17.0884161970686,20.5428350111995,19.7736738200008));
#192325=CARTESIAN_POINT('Ctrl Pts',(17.0968603405106,20.5532036758737,19.7744744286734));
#192326=CARTESIAN_POINT('Ctrl Pts',(17.1012603512762,20.5585526742631,19.7748901744508));
#192327=CARTESIAN_POINT('Ctrl Pts',(17.1126754383053,20.572291765164,19.7759651493995));
#192328=CARTESIAN_POINT('Ctrl Pts',(17.1197293575681,20.5806491850875,19.7766259608276));
#192329=CARTESIAN_POINT('Ctrl Pts',(17.1499117134608,20.615851909523,19.7794391960059));
#192330=CARTESIAN_POINT('Ctrl Pts',(17.1736463817918,20.6421676824092,19.7816166285068));
#192331=CARTESIAN_POINT('Ctrl Pts',(17.2376864189761,20.7096845787293,19.7874063402134));
#192332=CARTESIAN_POINT('Ctrl Pts',(17.2790311926336,20.7498549764321,19.7910611815857));
#192333=CARTESIAN_POINT('Ctrl Pts',(17.4217679794718,20.8776377509441,19.8033999130543));
#192334=CARTESIAN_POINT('Ctrl Pts',(17.529826925751,20.9573093523303,19.8123263237655));
#192335=CARTESIAN_POINT('Ctrl Pts',(17.7216270381622,21.0724091734604,19.8270271244417));
#192336=CARTESIAN_POINT('Ctrl Pts',(17.80144724644,21.1136540023846,19.8328476536774));
#192337=CARTESIAN_POINT('Ctrl Pts',(17.8924920045399,21.1535875654797,19.8389896565287));
#192338=CARTESIAN_POINT('Ctrl Pts',(17.9013574932526,21.1574040228163,19.8395826580494));
#192339=CARTESIAN_POINT('Ctrl Pts',(17.9144966605514,21.162954030924,19.8404537064101));
#192340=CARTESIAN_POINT('Ctrl Pts',(17.9187502547679,21.164734402634,19.8407344909505));
#192341=CARTESIAN_POINT('Ctrl Pts',(17.9263117552837,21.1678703274467,19.8412314564469));
#192342=CARTESIAN_POINT('Ctrl Pts',(17.929617307847,21.169231412355,19.841447969433));
#192343=CARTESIAN_POINT('Ctrl Pts',(17.9367125497266,21.1721319314229,19.8419111153251));
#192344=CARTESIAN_POINT('Ctrl Pts',(17.9405032468856,21.1736687530651,19.8421575900616));
#192345=CARTESIAN_POINT('Ctrl Pts',(17.9509339838556,21.1778624157423,19.8428332194433));
#192346=CARTESIAN_POINT('Ctrl Pts',(17.9575831405749,21.1804966392008,19.8432610306678));
#192347=CARTESIAN_POINT('Ctrl Pts',(17.9933579525023,21.1944603619384,19.8455480568529));
#192348=CARTESIAN_POINT('Ctrl Pts',(18.0227200880706,21.20517821939,19.8473727993063));
#192349=CARTESIAN_POINT('Ctrl Pts',(18.2073708574236,21.2679822392131,19.8585872814208));
#192350=CARTESIAN_POINT('Ctrl Pts',(18.3680441301276,21.3025551193941,19.8672421666823));
#192351=CARTESIAN_POINT('Ctrl Pts',(18.6477495096441,21.3294853917348,19.8826236758113));
#192352=CARTESIAN_POINT('Ctrl Pts',(18.7651027494354,21.3310110440876,19.8891640380702));
#192353=CARTESIAN_POINT('Ctrl Pts',(18.8962303216199,21.3218232170155,19.8968647194791));
#192354=CARTESIAN_POINT('Ctrl Pts',(18.9104790371467,21.3206797067965,19.8977064905335));
#192355=CARTESIAN_POINT('Ctrl Pts',(18.9331364609452,21.3186302271001,19.8990534126916));
#192356=CARTESIAN_POINT('Ctrl Pts',(18.9415533622446,21.3178180042235,19.8995556202262));
#192357=CARTESIAN_POINT('Ctrl Pts',(18.956388435896,21.3162966719657,19.9004441221694));
#192358=CARTESIAN_POINT('Ctrl Pts',(18.9628086892139,21.3156085801699,19.900829750119));
#192359=CARTESIAN_POINT('Ctrl Pts',(18.976080573831,21.3141247165323,19.9016292465067));
#192360=CARTESIAN_POINT('Ctrl Pts',(18.9829316571802,21.3133248097802,19.9020432410822));
#192361=CARTESIAN_POINT('Ctrl Pts',(19.0005059948045,21.3111857859422,19.9031085753757));
#192362=CARTESIAN_POINT('Ctrl Pts',(19.0112230288435,21.3097980289294,19.903761443622));
#192363=CARTESIAN_POINT('Ctrl Pts',(19.0558970773738,21.3036650139636,19.9064966551947));
#192364=CARTESIAN_POINT('Ctrl Pts',(19.0897453576836,21.2981774274413,19.9086023117608));
#192365=CARTESIAN_POINT('Ctrl Pts',(19.1775688371452,21.2817408814741,19.9141559136908));
#192366=CARTESIAN_POINT('Ctrl Pts',(19.2312738317926,21.2695040754118,19.9176422294214));
#192367=CARTESIAN_POINT('Ctrl Pts',(19.3900378934093,21.2267537787853,19.9282102873744));
#192368=CARTESIAN_POINT('Ctrl Pts',(19.4932690724207,21.1901806444038,19.9354404253612));
#192369=CARTESIAN_POINT('Ctrl Pts',(19.634390802547,21.1275114817911,19.9456404683942));
#192370=CARTESIAN_POINT('Ctrl Pts',(19.6749837641712,21.1079105393085,19.9486119402491));
#192371=CARTESIAN_POINT('Ctrl Pts',(19.7364749287004,21.0757585908294,19.9531456245587));
#192372=CARTESIAN_POINT('Ctrl Pts',(19.7578336592083,21.0641177206193,19.9547265542514));
#192373=CARTESIAN_POINT('Ctrl Pts',(19.7915869761196,21.0449598340191,19.9572299348011));
#192374=CARTESIAN_POINT('Ctrl Pts',(19.8041128999637,21.0376793051336,19.9581600680417));
#192375=CARTESIAN_POINT('Ctrl Pts',(19.8484719080412,21.0112833219707,19.9614555833422));
#192376=CARTESIAN_POINT('Ctrl Pts',(19.8798777158681,20.9914584579295,19.9637917492203));
#192377=CARTESIAN_POINT('Ctrl Pts',(19.9167022035744,20.9668347886799,19.9665197989439));
#192378=CARTESIAN_POINT('Ctrl Pts',(19.922636439096,20.9628229723573,19.9669590639339));
#192379=CARTESIAN_POINT('Ctrl Pts',(19.9322809326386,20.9562312813646,19.9676722333617));
#192380=CARTESIAN_POINT('Ctrl Pts',(19.9360034380581,20.9536695483513,19.9679473164054));
#192381=CARTESIAN_POINT('Ctrl Pts',(19.9426492444671,20.9490646488065,19.9684380578908));
#192382=CARTESIAN_POINT('Ctrl Pts',(19.9455756008995,20.9470260031171,19.9686540167094));
#192383=CARTESIAN_POINT('Ctrl Pts',(19.9518986256577,20.9425972934144,19.9691203547043));
#192384=CARTESIAN_POINT('Ctrl Pts',(19.9552934061132,20.9402046338719,19.969370552499));
#192385=CARTESIAN_POINT('Ctrl Pts',(19.964748380087,20.9334989845705,19.9700669672735));
#192386=CARTESIAN_POINT('Ctrl Pts',(19.9707929851895,20.9291639742603,19.9705117002635));
#192387=CARTESIAN_POINT('Ctrl Pts',(20.0056100942491,20.9039152356506,19.9730713354316));
#192388=CARTESIAN_POINT('Ctrl Pts',(20.03387654675,20.8823095244511,19.9751413066173));
#192389=CARTESIAN_POINT('Ctrl Pts',(20.1226969457606,20.8108014748794,19.9816669705971));
#192390=CARTESIAN_POINT('Ctrl Pts',(20.1810298673512,20.7582396210203,19.9859869949952));
#192391=CARTESIAN_POINT('Ctrl Pts',(20.3688915608898,20.5690230915093,20.0005307360924));
#192392=CARTESIAN_POINT('Ctrl Pts',(20.4830603932303,20.4184266466493,20.0105818978737));
#192393=CARTESIAN_POINT('Ctrl Pts',(20.5865933410782,20.2357262818972,20.0227986534416));
#192394=CARTESIAN_POINT('Ctrl Pts',(20.5970665410432,20.2165590740867,20.0240792321911));
#192395=CARTESIAN_POINT('Ctrl Pts',(20.6111621403572,20.1897860554178,20.0258679249136));
#192396=CARTESIAN_POINT('Ctrl Pts',(20.6150387543368,20.1823151110964,20.0263670485749));
#192397=CARTESIAN_POINT('Ctrl Pts',(20.6216328117126,20.1694196241617,20.0272286537558));
#192398=CARTESIAN_POINT('Ctrl Pts',(20.6243716967252,20.1640061148144,20.0275903770529));
#192399=CARTESIAN_POINT('Ctrl Pts',(20.6299765784718,20.1528086227341,20.0283386596843));
#192400=CARTESIAN_POINT('Ctrl Pts',(20.6328394636301,20.1470231609843,20.0287253230792));
#192401=CARTESIAN_POINT('Ctrl Pts',(20.6394509551753,20.1335071653448,20.0296287933117));
#192402=CARTESIAN_POINT('Ctrl Pts',(20.6431790309871,20.1257667664114,20.0301463084128));
#192403=CARTESIAN_POINT('Ctrl Pts',(20.6550044132437,20.1008271857208,20.0318142253026));
#192404=CARTESIAN_POINT('Ctrl Pts',(20.6629170329179,20.083541929807,20.0329709764449));
#192405=CARTESIAN_POINT('Ctrl Pts',(20.7015148573212,19.9961325578467,20.0388257950106));
#192406=CARTESIAN_POINT('Ctrl Pts',(20.72861048136,19.9244946414693,20.043644154093));
#192407=CARTESIAN_POINT('Ctrl Pts',(20.7850309776545,19.7467681221194,20.0556360630776));
#192408=CARTESIAN_POINT('Ctrl Pts',(20.8100805763456,19.6395575137347,20.0629079184764));
#192409=CARTESIAN_POINT('Ctrl Pts',(20.8373788536954,19.4609783705657,20.0748398799709));
#192410=CARTESIAN_POINT('Ctrl Pts',(20.8445566189063,19.3905648603529,20.0794962740809));
#192411=CARTESIAN_POINT('Ctrl Pts',(20.8506449076473,19.2723891232429,20.0871139899832));
#192412=CARTESIAN_POINT('Ctrl Pts',(20.8514902735322,19.2247838650631,20.0901289736452));
#192413=CARTESIAN_POINT('Ctrl Pts',(20.8506066481979,19.1694682112493,20.0935400235903));
#192414=CARTESIAN_POINT('Ctrl Pts',(20.8504411285165,19.1617501639017,20.0940138646602));
#192415=CARTESIAN_POINT('Ctrl Pts',(20.8501086334049,19.1493984864199,20.0947686451762));
#192416=CARTESIAN_POINT('Ctrl Pts',(20.8499686494859,19.144764283186,20.0950510326945));
#192417=CARTESIAN_POINT('Ctrl Pts',(20.8496933692947,19.136545772432,20.0955503727749));
#192418=CARTESIAN_POINT('Ctrl Pts',(20.8495641866245,19.1329613052336,20.0957676637308));
#192419=CARTESIAN_POINT('Ctrl Pts',(20.8492705657769,19.1253515144805,20.0962279082554));
#192420=CARTESIAN_POINT('Ctrl Pts',(20.8491037478303,19.1213263357981,20.096470727247));
#192421=CARTESIAN_POINT('Ctrl Pts',(20.8486212457494,19.1104354760286,20.097126082872));
#192422=CARTESIAN_POINT('Ctrl Pts',(20.8482836127381,19.1035707473647,20.0975374072481));
#192423=CARTESIAN_POINT('Ctrl Pts',(20.8464222024677,19.0691427258884,20.0995919961669));
#192424=CARTESIAN_POINT('Ctrl Pts',(20.844392755631,19.0416080598258,20.1012085538598));
#192425=CARTESIAN_POINT('Ctrl Pts',(20.8369190796479,18.9615940218318,20.105848778859));
#192426=CARTESIAN_POINT('Ctrl Pts',(20.8300509740369,18.9092665579418,20.1088114779129));
#192427=CARTESIAN_POINT('Ctrl Pts',(20.7977660018846,18.7187767986166,20.1195046036215));
#192428=CARTESIAN_POINT('Ctrl Pts',(20.7605765171409,18.5829843098432,20.1269707900731));
#192429=CARTESIAN_POINT('Ctrl Pts',(20.6769538441643,18.3652923313724,20.1398647528729));
#192430=CARTESIAN_POINT('Ctrl Pts',(20.6380460426288,18.2810017721445,20.1451035846945));
#192431=CARTESIAN_POINT('Ctrl Pts',(20.5871539680724,18.1874280943189,20.151347910443));
#192432=CARTESIAN_POINT('Ctrl Pts',(20.5804488810899,18.1753815414966,20.1521601887897));
#192433=CARTESIAN_POINT('Ctrl Pts',(20.5695155346613,18.1561821276042,20.1534686868267));
#192434=CARTESIAN_POINT('Ctrl Pts',(20.5653619288175,18.1489870506517,20.1539622228432));
#192435=CARTESIAN_POINT('Ctrl Pts',(20.5579168272317,18.1362638466598,20.1548406791175));
#192436=CARTESIAN_POINT('Ctrl Pts',(20.5546422631488,18.1307258958111,20.1552249813267));
#192437=CARTESIAN_POINT('Ctrl Pts',(20.5477720625339,18.1192269619934,20.1560270363756));
#192438=CARTESIAN_POINT('Ctrl Pts',(20.5441721700265,18.1132686237487,20.1564449416546));
#192439=CARTESIAN_POINT('Ctrl Pts',(20.5347581610594,18.0978593218574,20.1575317820132));
#192440=CARTESIAN_POINT('Ctrl Pts',(20.5288990662031,18.0884362117197,20.1582023663874));
#192441=CARTESIAN_POINT('Ctrl Pts',(20.5032384178612,18.0478810382046,20.1611146526714));
#192442=CARTESIAN_POINT('Ctrl Pts',(20.4826999273373,18.0172250656141,20.1633836083767));
#192443=CARTESIAN_POINT('Ctrl Pts',(20.4261259377924,17.9373769227243,20.1694794267445));
#192444=CARTESIAN_POINT('Ctrl Pts',(20.3887504048321,17.8891808210077,20.1733546605553));
#192445=CARTESIAN_POINT('Ctrl Pts',(20.2460841536001,17.7207597717741,20.1876064954377));
#192446=CARTESIAN_POINT('Ctrl Pts',(20.1293613244571,17.6109453342754,20.1983402021048));
#192447=CARTESIAN_POINT('Ctrl Pts',(19.9535183201071,17.4795155616797,20.212584583217));
#192448=CARTESIAN_POINT('Ctrl Pts',(19.9041312881027,17.4457641914325,20.2163996055444));
#192449=CARTESIAN_POINT('Ctrl Pts',(19.8457736883397,17.4094094489429,20.2206428440517));
#192450=CARTESIAN_POINT('Ctrl Pts',(19.8381401366158,17.4047210035659,20.2211928459624));
#192451=CARTESIAN_POINT('Ctrl Pts',(19.8265983438678,17.3977326680455,20.2220166028003));
#192452=CARTESIAN_POINT('Ctrl Pts',(19.8227122100215,17.3953967165732,20.2222926349463));
#192453=CARTESIAN_POINT('Ctrl Pts',(19.8157549108881,17.3912450601887,20.2227844018599));
#192454=CARTESIAN_POINT('Ctrl Pts',(19.8126866420369,17.3894246221711,20.22300044229));
#192455=CARTESIAN_POINT('Ctrl Pts',(19.8060460975571,17.3855073756232,20.2234662008151));
#192456=CARTESIAN_POINT('Ctrl Pts',(19.8024722768783,17.3834132985931,20.2237157415701));
#192457=CARTESIAN_POINT('Ctrl Pts',(19.7925074601183,17.3776136435188,20.2244084792046));
#192458=CARTESIAN_POINT('Ctrl Pts',(19.7861031076829,17.3739309676242,20.2248502174031));
#192459=CARTESIAN_POINT('Ctrl Pts',(19.7494580374532,17.3531135500383,20.2273587604739));
#192460=CARTESIAN_POINT('Ctrl Pts',(19.7188163475538,17.3366910170099,20.2293827060384));
#192461=CARTESIAN_POINT('Ctrl Pts',(19.6203559111956,17.2870025110269,20.2356997644838));
#192462=CARTESIAN_POINT('Ctrl Pts',(19.5511515493561,17.2566054018991,20.2398670157916));
#192463=CARTESIAN_POINT('Ctrl Pts',(19.3000572068204,17.1619912996553,20.2545191107828));
#192464=CARTESIAN_POINT('Ctrl Pts',(19.1112297217029,17.11897946783,20.2647930551012));
#192465=CARTESIAN_POINT('Ctrl Pts',(18.8979688673466,17.1002520111478,20.2772544091793));
#192466=CARTESIAN_POINT('Ctrl Pts',(18.8767201785455,17.098708882788,20.2785039623406));
#192467=CARTESIAN_POINT('Ctrl Pts',(18.8471370296364,17.0970088964751,20.2802560129076));
#192468=CARTESIAN_POINT('Ctrl Pts',(18.8388190312226,17.09658014081,20.2807500000378));
#192469=CARTESIAN_POINT('Ctrl Pts',(18.8244610976723,17.0959249848619,20.2816051097492));
#192470=CARTESIAN_POINT('Ctrl Pts',(18.818422283562,17.0956753424768,20.2819655005176));
#192471=CARTESIAN_POINT('Ctrl Pts',(18.8059186518273,17.0952120742832,20.2827132709647));
#192472=CARTESIAN_POINT('Ctrl Pts',(18.7994537654975,17.0950022111942,20.2831007646839));
#192473=CARTESIAN_POINT('Ctrl Pts',(18.7843172615155,17.0945802839226,20.2840100903042));
#192474=CARTESIAN_POINT('Ctrl Pts',(18.7756451482221,17.0943918833336,20.2845326583244));
#192475=CARTESIAN_POINT('Ctrl Pts',(18.7475081826927,17.0939535976432,20.2862334359272));
#192476=CARTESIAN_POINT('Ctrl Pts',(18.7280414207869,17.0939188970806,20.2874183505551));
#192477=CARTESIAN_POINT('Ctrl Pts',(18.6285949667789,17.0951132122844,20.29351518871));
#192478=CARTESIAN_POINT('Ctrl Pts',(18.5487404276439,17.1006058582918,20.2985588631999));
#192479=CARTESIAN_POINT('Ctrl Pts',(18.3723972888642,17.1228212624269,20.3100131654662));
#192480=CARTESIAN_POINT('Ctrl Pts',(18.2763681228698,17.141744676083,20.3164671589653));
#192481=CARTESIAN_POINT('Ctrl Pts',(18.0612387107882,17.1998491680736,20.3311923030113));
#192482=CARTESIAN_POINT('Ctrl Pts',(17.9435941958999,17.2431074206821,20.3394426661579));
#192483=CARTESIAN_POINT('Ctrl Pts',(17.8219457184588,17.3005198555948,20.3477493475554));
#192484=CARTESIAN_POINT('Ctrl Pts',(17.8134698778202,17.3045893159384,20.3483268093222));
#192485=CARTESIAN_POINT('Ctrl Pts',(17.8009218382442,17.3107171376273,20.3491794559844));
#192486=CARTESIAN_POINT('Ctrl Pts',(17.7968288621003,17.3127323497037,20.3494572174077));
#192487=CARTESIAN_POINT('Ctrl Pts',(17.7895445854272,17.3163481281665,20.3499508664201));
#192488=CARTESIAN_POINT('Ctrl Pts',(17.78635079617,17.317943547413,20.3501670692646));
#192489=CARTESIAN_POINT('Ctrl Pts',(17.7795515706867,17.321361538303,20.3506268270691));
#192490=CARTESIAN_POINT('Ctrl Pts',(17.775947323457,17.3231863466594,20.3508702389337));
#192491=CARTESIAN_POINT('Ctrl Pts',(17.7660977018342,17.3282086231039,20.3515346566113));
#192492=CARTESIAN_POINT('Ctrl Pts',(17.759862899825,17.331426872689,20.3519543782937));
#192493=CARTESIAN_POINT('Ctrl Pts',(17.7459578152103,17.3386921063875,20.3528887991308));
#192494=CARTESIAN_POINT('Ctrl Pts',(17.7382961244232,17.3427553679701,20.3534025287024));
#192495=CARTESIAN_POINT('Ctrl Pts',(17.7147287723702,17.3554401187007,20.3549799132406));
#192496=CARTESIAN_POINT('Ctrl Pts',(17.6989080902324,17.3642187212862,20.3560347793412));
#192497=CARTESIAN_POINT('Ctrl Pts',(17.6383226561558,17.398859633915,20.3600663122138));
#192498=CARTESIAN_POINT('Ctrl Pts',(17.5943958034201,17.4261569971446,20.3629722905541));
#192499=CARTESIAN_POINT('Ctrl Pts',(17.4369736985797,17.5321672644307,20.3734853469438));
#192500=CARTESIAN_POINT('Ctrl Pts',(17.3302571194892,17.6203193537634,20.3808298521585));
#192501=CARTESIAN_POINT('Ctrl Pts',(17.2120043418183,17.7392340795373,20.3900862402313));
#192502=CARTESIAN_POINT('Ctrl Pts',(17.1915692349662,17.760664534775,20.3917311305545));
#192503=CARTESIAN_POINT('Ctrl Pts',(17.1571320820595,17.798330288426,20.3945912674749));
#192504=CARTESIAN_POINT('Ctrl Pts',(17.1429146323016,17.8143628033448,20.3957994704802));
#192505=CARTESIAN_POINT('Ctrl Pts',(17.0965111966335,17.8683185987888,20.3998406338136));
#192506=CARTESIAN_POINT('Ctrl Pts',(17.0654202744549,17.9071579633068,20.4027101610731));
#192507=CARTESIAN_POINT('Ctrl Pts',(17.0281429210351,17.9572448386846,20.40638173292));
#192508=CARTESIAN_POINT('Ctrl Pts',(17.020650371766,17.9675035507768,20.4071322401939));
#192509=CARTESIAN_POINT('Ctrl Pts',(17.0089449006436,17.9838371975018,20.4083251152093));
#192510=CARTESIAN_POINT('Ctrl Pts',(17.004670615591,17.9898679359931,20.4087651114938));
#192511=CARTESIAN_POINT('Ctrl Pts',(16.9967775819607,18.0011290477236,20.4095859554126));
#192512=CARTESIAN_POINT('Ctrl Pts',(16.9931506404327,18.0063535967648,20.4099664834204));
#192513=CARTESIAN_POINT('Ctrl Pts',(16.985162515901,18.0179717723015,20.4108120677589));
#192514=CARTESIAN_POINT('Ctrl Pts',(16.9808127554928,18.0243731078845,20.4112775510116));
#192515=CARTESIAN_POINT('Ctrl Pts',(16.9683214435626,18.0429745882338,20.4126290795128));
#192516=CARTESIAN_POINT('Ctrl Pts',(16.9602715797871,18.0552354904494,20.4135185545034));
#192517=CARTESIAN_POINT('Ctrl Pts',(16.8994020535194,18.1500808520732,20.4203899755883));
#192518=CARTESIAN_POINT('Ctrl Pts',(16.8522561196807,18.2361490912158,20.4265808788633));
#192519=CARTESIAN_POINT('Ctrl Pts',(16.7513598311468,18.4551496144258,20.4421983674838));
#192520=CARTESIAN_POINT('Ctrl Pts',(16.7048136308439,18.5908626529497,20.4517799896776));
#192521=CARTESIAN_POINT('Ctrl Pts',(16.6660226853087,18.75720883082,20.4629186771635));
#192522=CARTESIAN_POINT('Ctrl Pts',(16.6602607809698,18.7843123468051,20.4647138075176));
#192523=CARTESIAN_POINT('Ctrl Pts',(16.6468711365671,18.8539948770933,20.4692668138028));
#192524=CARTESIAN_POINT('Ctrl Pts',(16.6400127083412,18.8967113399598,20.4719989740541));
#192525=CARTESIAN_POINT('Ctrl Pts',(16.6335056830049,18.9470513191892,20.4751271756401));
#192526=CARTESIAN_POINT('Ctrl Pts',(16.6325834879834,18.9544967277273,20.4755875030988));
#192527=CARTESIAN_POINT('Ctrl Pts',(16.6311572014184,18.9665362577807,20.4763279181513));
#192528=CARTESIAN_POINT('Ctrl Pts',(16.6306285495627,18.9711273270536,20.47660933514));
#192529=CARTESIAN_POINT('Ctrl Pts',(16.6297175168382,18.9792738303376,20.4771069988277));
#192530=CARTESIAN_POINT('Ctrl Pts',(16.6293291064467,18.9828285356172,20.4773235810695));
#192531=CARTESIAN_POINT('Ctrl Pts',(16.6285936556295,18.9897210230322,20.4777424113166));
#192532=CARTESIAN_POINT('Ctrl Pts',(16.6282455464677,18.9930586263391,20.4779447207648));
#192533=CARTESIAN_POINT('Ctrl Pts',(16.6274962892663,19.0004117718269,20.4783893508548));
#192534=CARTESIAN_POINT('Ctrl Pts',(16.6270986830446,19.0044276727148,20.4786314740247));
#192535=CARTESIAN_POINT('Ctrl Pts',(16.6261439843123,19.0143598980449,20.4792285971133));
#192536=CARTESIAN_POINT('Ctrl Pts',(16.6256003107858,19.0202775184922,20.4795828709947));
#192537=CARTESIAN_POINT('Ctrl Pts',(16.6234160991776,19.045203167999,20.4810691240488));
#192538=CARTESIAN_POINT('Ctrl Pts',(16.6220075782698,19.0642312782726,20.4821890740203));
#192539=CARTESIAN_POINT('Ctrl Pts',(16.618313691022,19.1253454546686,20.485746544444));
#192540=CARTESIAN_POINT('Ctrl Pts',(16.617027658706,19.167483096034,20.488139347873));
#192541=CARTESIAN_POINT('Ctrl Pts',(16.6170004413563,19.2096329951322,20.4904971933207));
#192542=CARTESIAN_POINT('Ctrl Pts',(16.7454193623258,19.9371102171621,20.5336910458214));
#192543=CARTESIAN_POINT('Ctrl Pts',(16.7207024854735,19.8694186993037,20.5293719537179));
#192544=CARTESIAN_POINT('Ctrl Pts',(16.6994546553919,19.8004872844824,20.5250528616144));
#192545=CARTESIAN_POINT('Ctrl Pts',(16.6817841755687,19.7307106983252,20.5207337695109));
#192546=CARTESIAN_POINT('Ctrl Pts',(16.664105969176,19.6609036017547,20.5164127888472));
#192547=CARTESIAN_POINT('Ctrl Pts',(16.6500083234449,19.5902510850496,20.5120918081835));
#192548=CARTESIAN_POINT('Ctrl Pts',(16.6395483092999,19.5191576144172,20.5077708275198));
#192549=CARTESIAN_POINT('Ctrl Pts',(16.6290728051449,19.4479588629934,20.5034434480088));
#192550=CARTESIAN_POINT('Ctrl Pts',(16.6222457279572,19.3763183482269,20.4991160684978));
#192551=CARTESIAN_POINT('Ctrl Pts',(16.6190721590219,19.3046441533458,20.4947886889867));
#192552=CARTESIAN_POINT('Ctrl Pts',(16.6176708338065,19.2729956028858,20.4928778856768));
#192553=CARTESIAN_POINT('Ctrl Pts',(16.6169811726879,19.2413404642854,20.4909670823669));
#192554=CARTESIAN_POINT('Ctrl Pts',(16.6170003908425,19.209713599163,20.489056279057));
#192555=CARTESIAN_POINT('Origin',(18.734,19.211,0.));
#192556=CARTESIAN_POINT('',(16.7454193623258,19.9371102171621,21.5555703650724));
#192557=CARTESIAN_POINT('',(16.7454193623258,19.9371102171621,21.3335535344094));
#192558=CARTESIAN_POINT('',(16.7454193623258,19.9371102171621,0.));
#192559=CARTESIAN_POINT('',(16.617000615865,19.2093852021581,21.5109437210328));
#192560=CARTESIAN_POINT('Ctrl Pts',(16.617000615865,19.2093852021581,21.5109437210328));
#192561=CARTESIAN_POINT('Ctrl Pts',(16.616945967273,19.2810294864738,21.5152671813527));
#192562=CARTESIAN_POINT('Ctrl Pts',(16.6205324536961,19.3528082880785,21.5195906416726));
#192563=CARTESIAN_POINT('Ctrl Pts',(16.6277745362619,19.424315015649,21.5239141019925));
#192564=CARTESIAN_POINT('Ctrl Pts',(16.6350090203951,19.4957467179695,21.5282330261142));
#192565=CARTESIAN_POINT('Ctrl Pts',(16.6458914490245,19.5669064212152,21.5325519502359));
#192566=CARTESIAN_POINT('Ctrl Pts',(16.6603842611256,19.6373880480177,21.5368708743575));
#192567=CARTESIAN_POINT('Ctrl Pts',(16.6748666461647,19.7078189658007,21.5411866911672));
#192568=CARTESIAN_POINT('Ctrl Pts',(16.6929541627611,19.7775722897502,21.5455025079768));
#192569=CARTESIAN_POINT('Ctrl Pts',(16.7145577235046,19.8462494721786,21.5498183247864));
#192570=CARTESIAN_POINT('Ctrl Pts',(16.7241553313425,19.8767600288495,21.5517356715484));
#192571=CARTESIAN_POINT('Ctrl Pts',(16.734446215425,19.9070583229105,21.5536530183104));
#192572=CARTESIAN_POINT('Ctrl Pts',(16.7454193623258,19.9371102171621,21.5555703650724));
#192573=CARTESIAN_POINT('Ctrl Pts',(16.6170005689228,19.209447963039,21.5099894604535));
#192574=CARTESIAN_POINT('Ctrl Pts',(16.6170514760726,19.1400099213996,21.5054225788889));
#192575=CARTESIAN_POINT('Ctrl Pts',(16.6205187490176,19.0706094573942,21.500900893449));
#192576=CARTESIAN_POINT('Ctrl Pts',(16.6297026242345,18.9782623033322,21.4950376253733));
#192577=CARTESIAN_POINT('Ctrl Pts',(16.6323979093154,18.9550643922718,21.493577929973));
#192578=CARTESIAN_POINT('Ctrl Pts',(16.636285362927,18.9258334914824,21.491759204291));
#192579=CARTESIAN_POINT('Ctrl Pts',(16.6371205628695,18.919755662051,21.4913821743009));
#192580=CARTESIAN_POINT('Ctrl Pts',(16.6385604188819,18.9096050541681,21.4907544778988));
#192581=CARTESIAN_POINT('Ctrl Pts',(16.6391505510601,18.9055302986921,21.490503036672));
#192582=CARTESIAN_POINT('Ctrl Pts',(16.6402462936381,18.8981169249711,21.4900465848008));
#192583=CARTESIAN_POINT('Ctrl Pts',(16.6407480096755,18.8947777570839,21.4898413593182));
#192584=CARTESIAN_POINT('Ctrl Pts',(16.6417946532316,18.8879234771462,21.4894208785397));
#192585=CARTESIAN_POINT('Ctrl Pts',(16.642340448676,18.8844085510559,21.4892056795509));
#192586=CARTESIAN_POINT('Ctrl Pts',(16.6435934062289,18.8764714851954,21.4887207018444));
#192587=CARTESIAN_POINT('Ctrl Pts',(16.6443057399722,18.8720502176448,21.4884512204746));
#192588=CARTESIAN_POINT('Ctrl Pts',(16.646501210917,18.8586935344663,21.4876390532523));
#192589=CARTESIAN_POINT('Ctrl Pts',(16.6480276910177,18.849765210832,21.4870987813851));
#192590=CARTESIAN_POINT('Ctrl Pts',(16.6601845708611,18.7813079893189,21.4829745480576));
#192591=CARTESIAN_POINT('Ctrl Pts',(16.6733049262745,18.722243505688,21.479522065513));
#192592=CARTESIAN_POINT('Ctrl Pts',(16.69382332133,18.6455573540763,21.4750843617421));
#192593=CARTESIAN_POINT('Ctrl Pts',(16.698953221487,18.6273640674337,21.4740349431003));
#192594=CARTESIAN_POINT('Ctrl Pts',(16.7159623154871,18.5699940119783,21.4707298273629));
#192595=CARTESIAN_POINT('Ctrl Pts',(16.7287346785616,18.5310912410399,21.4684945740175));
#192596=CARTESIAN_POINT('Ctrl Pts',(16.7545783257699,18.4594555531082,21.4643518724571));
#192597=CARTESIAN_POINT('Ctrl Pts',(16.7673541440347,18.4266319018062,21.4624429597118));
#192598=CARTESIAN_POINT('Ctrl Pts',(16.8090251671684,18.3269990333951,21.4565793428602));
#192599=CARTESIAN_POINT('Ctrl Pts',(16.8405503212018,18.2613508689022,21.4526165738847));
#192600=CARTESIAN_POINT('Ctrl Pts',(16.901831238818,18.1489753810926,21.4455036084311));
#192601=CARTESIAN_POINT('Ctrl Pts',(16.9301556402399,18.1015480928942,21.4423912319948));
#192602=CARTESIAN_POINT('Ctrl Pts',(16.9790290475463,18.0265410883997,21.4372424455897));
#192603=CARTESIAN_POINT('Ctrl Pts',(16.9984529420148,17.9982584079703,21.4352459079393));
#192604=CARTESIAN_POINT('Ctrl Pts',(17.0248610484141,17.9617406739852,21.4325885592976));
#192605=CARTESIAN_POINT('Ctrl Pts',(17.0312337451873,17.9530684063029,21.4319514421578));
#192606=CARTESIAN_POINT('Ctrl Pts',(17.0417740500905,17.9389515180439,21.4309041982852));
#192607=CARTESIAN_POINT('Ctrl Pts',(17.0459025254163,17.9334778199235,21.4304956127586));
#192608=CARTESIAN_POINT('Ctrl Pts',(17.0539413443128,17.9229266386452,21.4297030642932));
#192609=CARTESIAN_POINT('Ctrl Pts',(17.0578483025536,17.9178466616372,21.4293192384062));
#192610=CARTESIAN_POINT('Ctrl Pts',(17.066916242911,17.9061663144368,21.4284314703004));
#192611=CARTESIAN_POINT('Ctrl Pts',(17.0720934375547,17.8995787196105,21.4279268822287));
#192612=CARTESIAN_POINT('Ctrl Pts',(17.0861067058682,17.8819641238223,21.426567050121));
#192613=CARTESIAN_POINT('Ctrl Pts',(17.095014187257,17.8709947166758,21.4257089298295));
#192614=CARTESIAN_POINT('Ctrl Pts',(17.1997103751384,17.7446689066322,21.415692898114));
#192615=CARTESIAN_POINT('Ctrl Pts',(17.3073653772947,17.6397364542029,21.4060185248015));
#192616=CARTESIAN_POINT('Ctrl Pts',(17.4998881917639,17.4883007393238,21.3898623514561));
#192617=CARTESIAN_POINT('Ctrl Pts',(17.5784750964082,17.4346308209117,21.3835372371883));
#192618=CARTESIAN_POINT('Ctrl Pts',(17.6991993323576,17.3635956643708,21.3744154557351));
#192619=CARTESIAN_POINT('Ctrl Pts',(17.738715759255,17.3420096294588,21.3715176022211));
#192620=CARTESIAN_POINT('Ctrl Pts',(17.800914836807,17.3105658415141,21.3671223586442));
#192621=CARTESIAN_POINT('Ctrl Pts',(17.8231310027739,17.2998182434774,21.3655842077384));
#192622=CARTESIAN_POINT('Ctrl Pts',(17.8514871251667,17.2867071210671,21.3636655049593));
#192623=CARTESIAN_POINT('Ctrl Pts',(17.8574560074017,17.283980879744,21.3632640922076));
#192624=CARTESIAN_POINT('Ctrl Pts',(17.8664996722272,17.2799009693489,21.362659730934));
#192625=CARTESIAN_POINT('Ctrl Pts',(17.8695650933016,17.2785268236494,21.3624555410055));
#192626=CARTESIAN_POINT('Ctrl Pts',(17.8758766949369,17.2757155257917,21.3620365029449));
#192627=CARTESIAN_POINT('Ctrl Pts',(17.8791231719923,17.2742792633185,21.3618217173134));
#192628=CARTESIAN_POINT('Ctrl Pts',(17.8864141131182,17.2710756084496,21.3613410179091));
#192629=CARTESIAN_POINT('Ctrl Pts',(17.8904604959507,17.2693126960055,21.3610753803063));
#192630=CARTESIAN_POINT('Ctrl Pts',(17.9007717155665,17.2648586599681,21.3604013040124));
#192631=CARTESIAN_POINT('Ctrl Pts',(17.9070441483551,17.262185100722,21.3599939118205));
#192632=CARTESIAN_POINT('Ctrl Pts',(17.9427390879267,17.2471738720776,21.3576899943043));
#192633=CARTESIAN_POINT('Ctrl Pts',(17.9724263216596,17.2354715465259,21.3558294456741));
#192634=CARTESIAN_POINT('Ctrl Pts',(18.1885431807815,17.1558775597884,21.3426052557944));
#192635=CARTESIAN_POINT('Ctrl Pts',(18.3834491892948,17.1138150096998,21.3322947095244));
#192636=CARTESIAN_POINT('Ctrl Pts',(18.6371249752938,17.0954792997304,21.3181606270837));
#192637=CARTESIAN_POINT('Ctrl Pts',(18.6930030125068,17.093659408102,21.31501078714));
#192638=CARTESIAN_POINT('Ctrl Pts',(18.7835678678964,17.0942961952381,21.3098016666273));
#192639=CARTESIAN_POINT('Ctrl Pts',(18.8182380614379,17.0953923527782,21.3077829835726));
#192640=CARTESIAN_POINT('Ctrl Pts',(18.8637157581176,17.097949847093,21.3050967408519));
#192641=CARTESIAN_POINT('Ctrl Pts',(18.8745622019997,17.0986436410209,21.3044532160136));
#192642=CARTESIAN_POINT('Ctrl Pts',(18.8923074836142,17.0999159983177,21.3033955234311));
#192643=CARTESIAN_POINT('Ctrl Pts',(18.8992097611708,17.1004449415865,21.302982915038));
#192644=CARTESIAN_POINT('Ctrl Pts',(18.9125579805265,17.1015337380506,21.3021825985309));
#192645=CARTESIAN_POINT('Ctrl Pts',(18.9190042014731,17.1020893080285,21.3017950291851));
#192646=CARTESIAN_POINT('Ctrl Pts',(18.9338717259933,17.1034393621586,21.3008986184457));
#192647=CARTESIAN_POINT('Ctrl Pts',(18.9422909751693,17.1042547815511,21.3003891248679));
#192648=CARTESIAN_POINT('Ctrl Pts',(18.9648973958348,17.1065810899074,21.299015965141));
#192649=CARTESIAN_POINT('Ctrl Pts',(18.9790743668384,17.1081849592323,21.298149394373));
#192650=CARTESIAN_POINT('Ctrl Pts',(19.1068141531769,17.1239457375089,21.2902909631835));
#192651=CARTESIAN_POINT('Ctrl Pts',(19.2190528723219,17.1471438329611,21.2830110919086));
#192652=CARTESIAN_POINT('Ctrl Pts',(19.485928557976,17.2252809449586,21.2648702335341));
#192653=CARTESIAN_POINT('Ctrl Pts',(19.637136158265,17.2893284635313,21.2538526756614));
#192654=CARTESIAN_POINT('Ctrl Pts',(19.8079500251652,17.3863372344162,21.2413706015328));
#192655=CARTESIAN_POINT('Ctrl Pts',(19.8360674661234,17.4031807507792,21.2393166943286));
#192656=CARTESIAN_POINT('Ctrl Pts',(19.8699388353069,17.4245552270992,21.2368538794387));
#192657=CARTESIAN_POINT('Ctrl Pts',(19.8760735153067,17.4284708828906,21.236408290736));
#192658=CARTESIAN_POINT('Ctrl Pts',(19.8856566304435,17.4346573947448,21.2357131167827));
#192659=CARTESIAN_POINT('Ctrl Pts',(19.8891187550593,17.4369067927334,21.2354621522318));
#192660=CARTESIAN_POINT('Ctrl Pts',(19.895571236487,17.4411259693614,21.2349947972675));
#192661=CARTESIAN_POINT('Ctrl Pts',(19.8985631502955,17.4430931893779,21.234778247877));
#192662=CARTESIAN_POINT('Ctrl Pts',(19.9053763775538,17.4475977708323,21.2342854623733));
#192663=CARTESIAN_POINT('Ctrl Pts',(19.9091944350792,17.4501399600222,21.2340095540906));
#192664=CARTESIAN_POINT('Ctrl Pts',(19.9209018395014,17.4579901771666,21.2331641804027));
#192665=CARTESIAN_POINT('Ctrl Pts',(19.9287638362217,17.463339049233,21.2325973896085));
#192666=CARTESIAN_POINT('Ctrl Pts',(19.9989653003663,17.5117954202825,21.2275420480878));
#192667=CARTESIAN_POINT('Ctrl Pts',(20.0589911033888,17.5581737594304,21.2232589859039));
#192668=CARTESIAN_POINT('Ctrl Pts',(20.2235805178994,17.7000848672498,21.2112288497494));
#192669=CARTESIAN_POINT('Ctrl Pts',(20.3212210737501,17.8030063055925,21.2037065280896));
#192670=CARTESIAN_POINT('Ctrl Pts',(20.4457142238262,17.9637849230438,21.1924562739161));
#192671=CARTESIAN_POINT('Ctrl Pts',(20.4814021715165,18.0142979381967,21.1889868950583));
#192672=CARTESIAN_POINT('Ctrl Pts',(20.534976655748,18.0976443868653,21.1833006114781));
#192673=CARTESIAN_POINT('Ctrl Pts',(20.5542940631699,18.1295163386221,21.1811348534304));
#192674=CARTESIAN_POINT('Ctrl Pts',(20.5782796385727,18.1715551038524,21.1782817014748));
#192675=CARTESIAN_POINT('Ctrl Pts',(20.5837232566918,18.1812733644952,21.1776223762077));
#192676=CARTESIAN_POINT('Ctrl Pts',(20.5924495240457,18.1971444914772,21.1765458225672));
#192677=CARTESIAN_POINT('Ctrl Pts',(20.5957789560666,18.2032714936313,21.1761302720609));
#192678=CARTESIAN_POINT('Ctrl Pts',(20.6021221885369,18.2150833926388,21.1753292011754));
#192679=CARTESIAN_POINT('Ctrl Pts',(20.6051404656764,18.2207658072893,21.1749438456728));
#192680=CARTESIAN_POINT('Ctrl Pts',(20.6119901938784,18.2338047128863,21.1740596096595));
#192681=CARTESIAN_POINT('Ctrl Pts',(20.6158043914032,18.2411701041421,21.1735601263266));
#192682=CARTESIAN_POINT('Ctrl Pts',(20.6258186637318,18.260789630425,21.1722295424782));
#192683=CARTESIAN_POINT('Ctrl Pts',(20.6319428699606,18.2730818525524,21.1713957996083));
#192684=CARTESIAN_POINT('Ctrl Pts',(20.6774819003258,18.3667583305714,21.1650403574053));
#192685=CARTESIAN_POINT('Ctrl Pts',(20.7117604860588,18.4505227738403,21.1593418085756));
#192686=CARTESIAN_POINT('Ctrl Pts',(20.7851815471082,18.6688508430694,21.1444683312998));
#192687=CARTESIAN_POINT('Ctrl Pts',(20.8165229424175,18.8055808664268,21.1351170671379));
#192688=CARTESIAN_POINT('Ctrl Pts',(20.8410811064594,18.9990281702302,21.1223461872799));
#192689=CARTESIAN_POINT('Ctrl Pts',(20.8458832238423,19.053923819165,21.1187767409162));
#192690=CARTESIAN_POINT('Ctrl Pts',(20.8499084724558,19.1373275542845,21.1134918611606));
#192691=CARTESIAN_POINT('Ctrl Pts',(20.8507067453712,19.1657337773155,21.1117162147408));
#192692=CARTESIAN_POINT('Ctrl Pts',(20.8509881545861,19.2010862737162,21.1095435926542));
#192693=CARTESIAN_POINT('Ctrl Pts',(20.8510092759326,19.2080238748373,21.1091190200358));
#192694=CARTESIAN_POINT('Ctrl Pts',(20.8509887283658,19.2190041639062,21.108449997686));
#192695=CARTESIAN_POINT('Ctrl Pts',(20.8509695837611,19.2230467726219,21.1082043185368));
#192696=CARTESIAN_POINT('Ctrl Pts',(20.8509116410095,19.2306705320514,21.1077422325926));
#192697=CARTESIAN_POINT('Ctrl Pts',(20.8508753362383,19.23425159541,21.1075256948778));
#192698=CARTESIAN_POINT('Ctrl Pts',(20.8507715511013,19.242439219687,21.107031768043));
#192699=CARTESIAN_POINT('Ctrl Pts',(20.850698121036,19.2470456572814,21.1067547148771));
#192700=CARTESIAN_POINT('Ctrl Pts',(20.8504631980617,19.2592773272236,21.1060211746422));
#192701=CARTESIAN_POINT('Ctrl Pts',(20.8502755330337,19.2669020690511,21.1055661137596));
#192702=CARTESIAN_POINT('Ctrl Pts',(20.8486704995668,19.3203658250186,21.1023896725936));
#192703=CARTESIAN_POINT('Ctrl Pts',(20.8458050291108,19.3661528295392,21.0997434624873));
#192704=CARTESIAN_POINT('Ctrl Pts',(20.8378766748003,19.4493573627226,21.0950121637234));
#192705=CARTESIAN_POINT('Ctrl Pts',(20.8332965336635,19.4867999089902,21.0929118339656));
#192706=CARTESIAN_POINT('Ctrl Pts',(20.8083604781842,19.6535479897378,21.0836115746201));
#192707=CARTESIAN_POINT('Ctrl Pts',(20.777039847047,19.7809208510916,21.0766341036281));
#192708=CARTESIAN_POINT('Ctrl Pts',(20.7052145667264,19.9880492344194,21.0645333293891));
#192709=CARTESIAN_POINT('Ctrl Pts',(20.6710806061883,20.069608490702,21.05956122565));
#192710=CARTESIAN_POINT('Ctrl Pts',(20.6228634555686,20.1671930277235,21.0532176312391));
#192711=CARTESIAN_POINT('Ctrl Pts',(20.6135045550156,20.185460283434,21.0520126115572));
#192712=CARTESIAN_POINT('Ctrl Pts',(20.5997293509222,20.2114106273785,21.0502742603882));
#192713=CARTESIAN_POINT('Ctrl Pts',(20.5955279349911,20.2192069122344,21.0497485338322));
#192714=CARTESIAN_POINT('Ctrl Pts',(20.5881610574298,20.2326740915707,21.0488342642214));
#192715=CARTESIAN_POINT('Ctrl Pts',(20.5850181696237,20.2383572458244,21.0484465314966));
#192716=CARTESIAN_POINT('Ctrl Pts',(20.5789259099609,20.2492549186532,21.0476993172978));
#192717=CARTESIAN_POINT('Ctrl Pts',(20.5759804522534,20.254471562488,21.0473399793536));
#192718=CARTESIAN_POINT('Ctrl Pts',(20.5682085306612,20.2681008147428,21.0463967827888));
#192719=CARTESIAN_POINT('Ctrl Pts',(20.5633463682453,20.2764928092513,21.0458116367754));
#192720=CARTESIAN_POINT('Ctrl Pts',(20.5462830669485,20.3054826263244,21.043774809955));
#192721=CARTESIAN_POINT('Ctrl Pts',(20.5337906762122,20.325906086627,21.0423125560804));
#192722=CARTESIAN_POINT('Ctrl Pts',(20.437687778471,20.477196403204,21.0312701560227));
#192723=CARTESIAN_POINT('Ctrl Pts',(20.3402647137796,20.5986968239619,21.0211538266253));
#192724=CARTESIAN_POINT('Ctrl Pts',(20.1778790644151,20.7609766117255,21.0059869580296));
#192725=CARTESIAN_POINT('Ctrl Pts',(20.1225691328863,20.8107157759639,21.0010639088933));
#192726=CARTESIAN_POINT('Ctrl Pts',(20.0289987656021,20.8863450692377,20.9932278344425));
#192727=CARTESIAN_POINT('Ctrl Pts',(19.9923066925104,20.9140759575389,20.9902670127103));
#192728=CARTESIAN_POINT('Ctrl Pts',(19.9410819425929,20.9502301708068,20.986312332158));
#192729=CARTESIAN_POINT('Ctrl Pts',(19.92731134,20.959707089788,20.9852661621551));
#192730=CARTESIAN_POINT('Ctrl Pts',(19.9035328193865,20.9756597439225,20.9834904436081));
#192731=CARTESIAN_POINT('Ctrl Pts',(19.893579995448,20.9822157622976,20.9827562488977));
#192732=CARTESIAN_POINT('Ctrl Pts',(19.8793558083444,20.9914140763217,20.9817203715126));
#192733=CARTESIAN_POINT('Ctrl Pts',(19.875129800612,20.9941256237914,20.9814142770875));
#192734=CARTESIAN_POINT('Ctrl Pts',(19.8678311471682,20.9987721090739,20.9808885453356));
#192735=CARTESIAN_POINT('Ctrl Pts',(19.8647631118735,21.0007142145842,20.9806684349348));
#192736=CARTESIAN_POINT('Ctrl Pts',(19.8588032234887,21.0044654564925,20.9802425849374));
#192737=CARTESIAN_POINT('Ctrl Pts',(19.8559119978918,21.0062754954517,20.9800367823656));
#192738=CARTESIAN_POINT('Ctrl Pts',(19.8481023485937,21.011138457909,20.9794829514067));
#192739=CARTESIAN_POINT('Ctrl Pts',(19.8431757149041,21.0141782346854,20.9791357841421));
#192740=CARTESIAN_POINT('Ctrl Pts',(19.8248600813388,21.0253756755394,20.9778530679902));
#192741=CARTESIAN_POINT('Ctrl Pts',(19.8113926771083,21.0334049661969,20.9769255568403));
#192742=CARTESIAN_POINT('Ctrl Pts',(19.6817603879085,21.1087526156303,20.9681342432055));
#192743=CARTESIAN_POINT('Ctrl Pts',(19.5595120547503,21.1650354409874,20.9608717268428));
#192744=CARTESIAN_POINT('Ctrl Pts',(19.2810476021562,21.2624024974086,20.9448519793377));
#192745=CARTESIAN_POINT('Ctrl Pts',(19.1238298381548,21.2979925293925,20.9361046021643));
#192746=CARTESIAN_POINT('Ctrl Pts',(18.9455576821849,21.3174853595901,20.925631613753));
#192747=CARTESIAN_POINT('Ctrl Pts',(18.9269819602058,21.3192682829984,20.9245344899101));
#192748=CARTESIAN_POINT('Ctrl Pts',(18.8998852282073,21.3215079577503,20.9229246643101));
#192749=CARTESIAN_POINT('Ctrl Pts',(18.8913808605586,21.3221591626752,20.9224180679968));
#192750=CARTESIAN_POINT('Ctrl Pts',(18.8764413407627,21.3232123555081,20.9215256795755));
#192751=CARTESIAN_POINT('Ctrl Pts',(18.8700078158853,21.3236363726203,20.9211405841363));
#192752=CARTESIAN_POINT('Ctrl Pts',(18.8574952526817,21.3244036515734,20.9203900205283));
#192753=CARTESIAN_POINT('Ctrl Pts',(18.8514164671774,21.3247500902306,20.9200246560614));
#192754=CARTESIAN_POINT('Ctrl Pts',(18.8368546841907,21.3255169783241,20.9191476392207));
#192755=CARTESIAN_POINT('Ctrl Pts',(18.8283705349422,21.3259126073027,20.9186352131181));
#192756=CARTESIAN_POINT('Ctrl Pts',(18.7975861841148,21.3271625231008,20.9167705151548));
#192757=CARTESIAN_POINT('Ctrl Pts',(18.7752758197653,21.3277152084991,20.915408848518));
#192758=CARTESIAN_POINT('Ctrl Pts',(18.5696370345954,21.3295571469673,20.9027594061675));
#192759=CARTESIAN_POINT('Ctrl Pts',(18.386908382201,21.3073779179333,20.8906947602941));
#192760=CARTESIAN_POINT('Ctrl Pts',(18.1303749379129,21.2417569008552,20.8732106831505));
#192761=CARTESIAN_POINT('Ctrl Pts',(18.0526120479145,21.2170032458207,20.8678505622162));
#192762=CARTESIAN_POINT('Ctrl Pts',(17.9424737730587,21.1747974520506,20.8603296315121));
#192763=CARTESIAN_POINT('Ctrl Pts',(17.9088201110924,21.1608955664088,20.8580419950872));
#192764=CARTESIAN_POINT('Ctrl Pts',(17.868691236688,21.143093650157,20.8553410489813));
#192765=CARTESIAN_POINT('Ctrl Pts',(17.8618589949675,21.1400192326766,20.8548821489732));
#192766=CARTESIAN_POINT('Ctrl Pts',(17.8512527076488,21.1351786760659,20.8541714152479));
#192767=CARTESIAN_POINT('Ctrl Pts',(17.8474673905208,21.1334375913408,20.8539180889712));
#192768=CARTESIAN_POINT('Ctrl Pts',(17.8404512609386,21.1301853407585,20.8534491934583));
#192769=CARTESIAN_POINT('Ctrl Pts',(17.8372191560386,21.1286771989723,20.8532334482913));
#192770=CARTESIAN_POINT('Ctrl Pts',(17.8299130095227,21.1252455460227,20.852746334506));
#192771=CARTESIAN_POINT('Ctrl Pts',(17.8258412984364,21.1233171992257,20.8524752689658));
#192772=CARTESIAN_POINT('Ctrl Pts',(17.8135516410723,21.1174487604509,20.8516582382603));
#192773=CARTESIAN_POINT('Ctrl Pts',(17.8053528288313,21.1134685269139,20.8511146998513));
#192774=CARTESIAN_POINT('Ctrl Pts',(17.7424061816535,21.0824062688924,20.8469515340594));
#192775=CARTESIAN_POINT('Ctrl Pts',(17.6888224192078,21.0530165623255,20.8434650796795));
#192776=CARTESIAN_POINT('Ctrl Pts',(17.4971412875124,20.9368208088771,20.8309358219835));
#192777=CARTESIAN_POINT('Ctrl Pts',(17.3679309893915,20.8364655076265,20.8223347994012));
#192778=CARTESIAN_POINT('Ctrl Pts',(17.1948920375277,20.6667222325276,20.8088862591062));
#192779=CARTESIAN_POINT('Ctrl Pts',(17.1414400752061,20.608043829206,20.8043989483772));
#192780=CARTESIAN_POINT('Ctrl Pts',(17.0791842625823,20.5314731773872,20.7986403046093));
#192781=CARTESIAN_POINT('Ctrl Pts',(17.0671665107565,20.5162703242046,20.7975015757591));
#192782=CARTESIAN_POINT('Ctrl Pts',(17.0500837117325,20.494039323221,20.7958420189092));
#192783=CARTESIAN_POINT('Ctrl Pts',(17.0448502079753,20.4871414292824,20.7953278534071));
#192784=CARTESIAN_POINT('Ctrl Pts',(17.0357826740992,20.4750366776844,20.794426810133));
#192785=CARTESIAN_POINT('Ctrl Pts',(17.0319298852444,20.469843966322,20.794040673272));
#192786=CARTESIAN_POINT('Ctrl Pts',(17.0245192153108,20.4597597971696,20.7932915220662));
#192787=CARTESIAN_POINT('Ctrl Pts',(17.0209583857795,20.4548705764736,20.7929286275567));
#192788=CARTESIAN_POINT('Ctrl Pts',(17.0125342137011,20.4431989286185,20.7920630537975));
#192789=CARTESIAN_POINT('Ctrl Pts',(17.007689957473,20.4364029080416,20.7915596447327));
#192790=CARTESIAN_POINT('Ctrl Pts',(16.9905653835099,20.412075719693,20.7897595896725));
#192791=CARTESIAN_POINT('Ctrl Pts',(16.9785112285648,20.3943876233003,20.7884543683578));
#192792=CARTESIAN_POINT('Ctrl Pts',(16.8760651329884,20.2390491443778,20.7770190350146));
#192793=CARTESIAN_POINT('Ctrl Pts',(16.801817613528,20.0915667584953,20.7662792900608));
#192794=CARTESIAN_POINT('Ctrl Pts',(16.7454193572565,19.9371102032791,20.755413683557));
#192795=CARTESIAN_POINT('',(16.6170002905218,19.2098909150927,21.2890562789773));
#192796=CARTESIAN_POINT('Ctrl Pts',(16.6170002905218,19.2098909150927,21.2890562789773));
#192797=CARTESIAN_POINT('Ctrl Pts',(16.6170426459466,19.1290437037364,21.2842160179537));
#192798=CARTESIAN_POINT('Ctrl Pts',(16.6217204203657,19.0483585462384,21.2793757569302));
#192799=CARTESIAN_POINT('Ctrl Pts',(16.6309534063534,18.9683396922623,21.2745354959067));
#192800=CARTESIAN_POINT('Ctrl Pts',(16.6402204417599,18.888025744643,21.2696773849617));
#192801=CARTESIAN_POINT('Ctrl Pts',(16.6540762126097,18.8083833014798,21.2648192740168));
#192802=CARTESIAN_POINT('Ctrl Pts',(16.6723897133774,18.7299053875882,21.2599611630718));
#192803=CARTESIAN_POINT('Ctrl Pts',(16.6907932588013,18.6510416099083,21.2550791655452));
#192804=CARTESIAN_POINT('Ctrl Pts',(16.7136983382303,18.5733541106456,21.2501971680187));
#192805=CARTESIAN_POINT('Ctrl Pts',(16.7409237582267,18.4973221353589,21.2453151704921));
#192806=CARTESIAN_POINT('Ctrl Pts',(16.7538532455414,18.4612141722819,21.2429966855946));
#192807=CARTESIAN_POINT('Ctrl Pts',(16.7677564325119,18.4254792559445,21.2406782006971));
#192808=CARTESIAN_POINT('Ctrl Pts',(16.7826102744629,18.3901668019212,21.2383597157996));
#192809=CARTESIAN_POINT('Ctrl Pts',(16.8107255793529,18.3233275010485,21.2339712949458));
#192810=CARTESIAN_POINT('Ctrl Pts',(16.8423337821689,18.2578040117701,21.229582874092));
#192811=CARTESIAN_POINT('Ctrl Pts',(16.8772900899987,18.1939860816573,21.2251944532382));
#192812=CARTESIAN_POINT('Ctrl Pts',(16.9121945317766,18.130262840723,21.2208125436574));
#192813=CARTESIAN_POINT('Ctrl Pts',(16.9504369871457,18.068240554869,21.2164306340766));
#192814=CARTESIAN_POINT('Ctrl Pts',(16.9918247580849,18.0082887185787,21.2120487244958));
#192815=CARTESIAN_POINT('Ctrl Pts',(17.0331639095237,17.9484073095731,21.2076719624803));
#192816=CARTESIAN_POINT('Ctrl Pts',(17.077640763908,17.8905919134513,21.2032952004649));
#192817=CARTESIAN_POINT('Ctrl Pts',(17.1250177563768,17.8351856448978,21.1989184384494));
#192818=CARTESIAN_POINT('Ctrl Pts',(17.1723647117999,17.7798145039565,21.194544451304));
#192819=CARTESIAN_POINT('Ctrl Pts',(17.2226078444088,17.7268498257148,21.1901704641587));
#192820=CARTESIAN_POINT('Ctrl Pts',(17.2754683616743,17.6766029001582,21.1857964770133));
#192821=CARTESIAN_POINT('Ctrl Pts',(17.3283127983901,17.6263712600779,21.1814238204663));
#192822=CARTESIAN_POINT('Ctrl Pts',(17.3837726896225,17.5788560634065,21.1770511639194));
#192823=CARTESIAN_POINT('Ctrl Pts',(17.4415325011772,17.5343316474368,21.1726785073724));
#192824=CARTESIAN_POINT('Ctrl Pts',(17.4992937900869,17.4898060926414,21.1683057389835));
#192825=CARTESIAN_POINT('Ctrl Pts',(17.5593547328911,17.4482717633095,21.1639329705946));
#192826=CARTESIAN_POINT('Ctrl Pts',(17.6213681875234,17.4099615634682,21.1595602022058));
#192827=CARTESIAN_POINT('Ctrl Pts',(17.6834459783432,17.3716116185067,21.1551828972651));
#192828=CARTESIAN_POINT('Ctrl Pts',(17.7474799141124,17.3364927353749,21.1508055923245));
#192829=CARTESIAN_POINT('Ctrl Pts',(17.8130961612385,17.3047930018609,21.1464282873839));
#192830=CARTESIAN_POINT('Ctrl Pts',(17.8787482349071,17.2730759602579,21.14204859243));
#192831=CARTESIAN_POINT('Ctrl Pts',(17.9459838951715,17.2447819724004,21.1376688974761));
#192832=CARTESIAN_POINT('Ctrl Pts',(18.0144096407929,17.2200508005134,21.1332892025222));
#192833=CARTESIAN_POINT('Ctrl Pts',(18.0829566152675,17.1952758127853,21.1289017481293));
#192834=CARTESIAN_POINT('Ctrl Pts',(18.1526974237226,17.1740763866221,21.1245142937365));
#192835=CARTESIAN_POINT('Ctrl Pts',(18.2232243074044,17.1565421172841,21.1201268393436));
#192836=CARTESIAN_POINT('Ctrl Pts',(18.271142526286,17.1446287742835,21.1171458626018));
#192837=CARTESIAN_POINT('Ctrl Pts',(18.3194233700504,17.1344063045172,21.1141648858599));
#192838=CARTESIAN_POINT('Ctrl Pts',(18.3679374553786,17.1258891603981,21.1111839091181));
#192839=CARTESIAN_POINT('Ctrl Pts',(18.4393551977364,17.1133510449166,21.1067956035882));
#192840=CARTESIAN_POINT('Ctrl Pts',(18.511557184181,17.1044619384225,21.1024072980583));
#192841=CARTESIAN_POINT('Ctrl Pts',(18.584137344166,17.0993110588,21.0980189925284));
#192842=CARTESIAN_POINT('Ctrl Pts',(18.6566098256394,17.0941678209222,21.0936371974031));
#192843=CARTESIAN_POINT('Ctrl Pts',(18.7294588897195,17.0927518342718,21.0892554022779));
#192844=CARTESIAN_POINT('Ctrl Pts',(18.8022695645398,17.0951010736433,21.0848736071526));
#192845=CARTESIAN_POINT('Ctrl Pts',(18.874994735323,17.0974475542235,21.0804969577174));
#192846=CARTESIAN_POINT('Ctrl Pts',(18.9476811266901,17.1035504617408,21.0761203082823));
#192847=CARTESIAN_POINT('Ctrl Pts',(19.0199116617327,17.113395766193,21.0717436588472));
#192848=CARTESIAN_POINT('Ctrl Pts',(19.0920964214468,17.1232348312887,21.0673697830668));
#192849=CARTESIAN_POINT('Ctrl Pts',(19.1638254212813,17.1368115225586,21.0629959072864));
#192850=CARTESIAN_POINT('Ctrl Pts',(19.2346860280265,17.1540599179026,21.058622031506));
#192851=CARTESIAN_POINT('Ctrl Pts',(19.3055251003311,17.171303071483,21.0542494849405));
#192852=CARTESIAN_POINT('Ctrl Pts',(19.3754958350899,17.1922155998631,21.0498769383749));
#192853=CARTESIAN_POINT('Ctrl Pts',(19.4441967831924,17.2166806852605,21.0455043918093));
#192854=CARTESIAN_POINT('Ctrl Pts',(19.5128995129431,17.2411464051203,21.0411317318488));
#192855=CARTESIAN_POINT('Ctrl Pts',(19.5803319369287,17.2691647012125,21.0367590718883));
#192856=CARTESIAN_POINT('Ctrl Pts',(19.6461103367674,17.3005697517151,21.0323864119278));
#192857=CARTESIAN_POINT('Ctrl Pts',(19.7119570281094,17.332007407117,21.0280092122472));
#192858=CARTESIAN_POINT('Ctrl Pts',(19.7761458305496,17.3668386288833,21.0236320125666));
#192859=CARTESIAN_POINT('Ctrl Pts',(19.8383162620759,17.4048508939418,21.019254812886));
#192860=CARTESIAN_POINT('Ctrl Pts',(19.9005206624135,17.4428839282218,21.0148752215819));
#192861=CARTESIAN_POINT('Ctrl Pts',(19.9607040979254,17.4841011935237,21.0104956302777));
#192862=CARTESIAN_POINT('Ctrl Pts',(20.0185360763143,17.5282474725477,21.0061160389735));
#192863=CARTESIAN_POINT('Ctrl Pts',(20.0764705669914,17.5724720047493,21.0017286844571));
#192864=CARTESIAN_POINT('Ctrl Pts',(20.1320449087986,17.6196356063735,20.9973413299406));
#192865=CARTESIAN_POINT('Ctrl Pts',(20.1849630756626,17.6694439182878,20.9929539754242));
#192866=CARTESIAN_POINT('Ctrl Pts',(20.2209300194265,17.7032971838063,20.9899720177616));
#192867=CARTESIAN_POINT('Ctrl Pts',(20.2556706966756,17.7383713940979,20.9869900600991));
#192868=CARTESIAN_POINT('Ctrl Pts',(20.2891028445139,17.7745654755664,20.9840081024366));
#192869=CARTESIAN_POINT('Ctrl Pts',(20.3382998967395,17.8278268491664,20.9796200048616));
#192870=CARTESIAN_POINT('Ctrl Pts',(20.3848536073391,17.8837226211078,20.9752319072866));
#192871=CARTESIAN_POINT('Ctrl Pts',(20.4284691550635,17.9419597001914,20.9708438097116));
#192872=CARTESIAN_POINT('Ctrl Pts',(20.4720199507418,18.000110319968,20.9664622267469));
#192873=CARTESIAN_POINT('Ctrl Pts',(20.5126409559541,18.0605949637829,20.9620806437822));
#192874=CARTESIAN_POINT('Ctrl Pts',(20.5500756142482,18.1230853143131,20.9576990608175));
#192875=CARTESIAN_POINT('Ctrl Pts',(20.5874662646494,18.1855022016739,20.9533226288076));
#192876=CARTESIAN_POINT('Ctrl Pts',(20.6216777625938,18.2499197000074,20.9489461967977));
#192877=CARTESIAN_POINT('Ctrl Pts',(20.6524961368915,18.3159795685391,20.9445697647878));
#192878=CARTESIAN_POINT('Ctrl Pts',(20.6832949573685,18.3819975230225,20.9401961095618));
#192879=CARTESIAN_POINT('Ctrl Pts',(20.7107047223526,18.449655344029,20.9358224543359));
#192880=CARTESIAN_POINT('Ctrl Pts',(20.7345574965437,18.5185704346126,20.9314487991099));
#192881=CARTESIAN_POINT('Ctrl Pts',(20.7584030062156,18.587464536652,20.9270764759094));
#192882=CARTESIAN_POINT('Ctrl Pts',(20.7786935180933,18.6576146924788,20.922704152709));
#192883=CARTESIAN_POINT('Ctrl Pts',(20.7953099442832,18.7286201563092,20.9183318295085));
#192884=CARTESIAN_POINT('Ctrl Pts',(20.8119267919329,18.7996274211253,20.9139593954082));
#192885=CARTESIAN_POINT('Ctrl Pts',(20.8248692609018,18.871489566845,20.9095869613079));
#192886=CARTESIAN_POINT('Ctrl Pts',(20.8340690644341,18.9437942279684,20.9052145272077));
#192887=CARTESIAN_POINT('Ctrl Pts',(20.8432784149155,19.0161739220992,20.9008375556837));
#192888=CARTESIAN_POINT('Ctrl Pts',(20.8487372844885,19.0889965689121,20.8964605841598));
#192889=CARTESIAN_POINT('Ctrl Pts',(20.8504292318751,19.161844059721,20.8920836126359));
#192890=CARTESIAN_POINT('Ctrl Pts',(20.8521221031259,19.2347313278874,20.8877042511276));
#192891=CARTESIAN_POINT('Ctrl Pts',(20.8500439707311,19.3076429845142,20.8833248896193));
#192892=CARTESIAN_POINT('Ctrl Pts',(20.8442305254939,19.3801630257289,20.8789455281111));
#192893=CARTESIAN_POINT('Ctrl Pts',(20.8384067750087,19.4528116201468,20.8745584034943));
#192894=CARTESIAN_POINT('Ctrl Pts',(20.8288345523668,19.5250667342145,20.8701712788775));
#192895=CARTESIAN_POINT('Ctrl Pts',(20.8156011167307,19.5965201561856,20.8657841542607));
#192896=CARTESIAN_POINT('Ctrl Pts',(20.8066002445799,19.6451200159337,20.8628002014256));
#192897=CARTESIAN_POINT('Ctrl Pts',(20.7959066968999,19.6933492110076,20.8598162485904));
#192898=CARTESIAN_POINT('Ctrl Pts',(20.7835610193857,19.7410836045517,20.8568322957552));
#192899=CARTESIAN_POINT('Ctrl Pts',(20.7654052821597,19.8112825146428,20.8524440502735));
#192900=CARTESIAN_POINT('Ctrl Pts',(20.7436033946027,19.8806845840498,20.8480558047918));
#192901=CARTESIAN_POINT('Ctrl Pts',(20.7182422505467,19.9488832503489,20.8436675593101));
#192902=CARTESIAN_POINT('Ctrl Pts',(20.6929187443098,20.0169807047679,20.8392858263103));
#192903=CARTESIAN_POINT('Ctrl Pts',(20.6640466342099,20.0838778530322,20.8349040933104));
#192904=CARTESIAN_POINT('Ctrl Pts',(20.6317631447894,20.1491812438324,20.8305223603105));
#192905=CARTESIAN_POINT('Ctrl Pts',(20.5995175882209,20.2144079036502,20.8261457758132));
#192906=CARTESIAN_POINT('Ctrl Pts',(20.5638688276462,20.2780440957741,20.821769191316));
#192907=CARTESIAN_POINT('Ctrl Pts',(20.52500229796,20.3397159823012,20.8173926068187));
#192908=CARTESIAN_POINT('Ctrl Pts',(20.4861604149721,20.401348760413,20.8130187976749));
#192909=CARTESIAN_POINT('Ctrl Pts',(20.4441050680544,20.4610192973534,20.8086449885311));
#192910=CARTESIAN_POINT('Ctrl Pts',(20.3990670887796,20.5183792830939,20.8042711793873));
#192911=CARTESIAN_POINT('Ctrl Pts',(20.3540428132133,20.5757218159082,20.7998987010627));
#192912=CARTESIAN_POINT('Ctrl Pts',(20.3060380047229,20.6307548140923,20.7955262227381));
#192913=CARTESIAN_POINT('Ctrl Pts',(20.2553251939663,20.6831612188219,20.7911537444134));
#192914=CARTESIAN_POINT('Ctrl Pts',(20.2046110855668,20.7355689645303,20.7867811542055));
#192915=CARTESIAN_POINT('Ctrl Pts',(20.1511891742029,20.7853496380956,20.7824085639976));
#192916=CARTESIAN_POINT('Ctrl Pts',(20.0953692572892,20.8322226081905,20.7780359737897));
#192917=CARTESIAN_POINT('Ctrl Pts',(20.039491410639,20.8791442229081,20.7736588457212));
#192918=CARTESIAN_POINT('Ctrl Pts',(19.9812109598893,20.9231517984441,20.7692817176527));
#192919=CARTESIAN_POINT('Ctrl Pts',(19.9208705934444,20.9640051895009,20.7649045895843));
#192920=CARTESIAN_POINT('Ctrl Pts',(19.8604972734422,21.004880891734,20.7605250710441));
#192921=CARTESIAN_POINT('Ctrl Pts',(19.7980622110869,21.0425987302322,20.7561455525039));
#192922=CARTESIAN_POINT('Ctrl Pts',(19.7339345423434,21.0769635342173,20.7517660339637));
#192923=CARTESIAN_POINT('Ctrl Pts',(19.6696932153011,21.1113892455334,20.7473787532728));
#192924=CARTESIAN_POINT('Ctrl Pts',(19.6037537278872,21.1424498489971,20.742991472582));
#192925=CARTESIAN_POINT('Ctrl Pts',(19.5365065764868,21.1699977526009,20.7386041918911));
#192926=CARTESIAN_POINT('Ctrl Pts',(19.4907905192111,21.1887254089068,20.7356216242854));
#192927=CARTESIAN_POINT('Ctrl Pts',(19.444470516459,21.2058306634918,20.7326390566796));
#192928=CARTESIAN_POINT('Ctrl Pts',(19.3976727117749,21.221280460942,20.7296564890738));
#192929=CARTESIAN_POINT('Ctrl Pts',(19.3288196246099,21.2440115753118,20.7252682706793));
#192930=CARTESIAN_POINT('Ctrl Pts',(19.258662966693,21.2632455878281,20.7208800522848));
#192931=CARTESIAN_POINT('Ctrl Pts',(19.1875916213885,21.2788354966017,20.7164918338903));
#192932=CARTESIAN_POINT('Ctrl Pts',(19.1166257529093,21.2944022684265,20.712110128041));
#192933=CARTESIAN_POINT('Ctrl Pts',(19.0447483591154,21.3063355700378,20.7077284221917));
#192934=CARTESIAN_POINT('Ctrl Pts',(18.9723645424585,21.31453781637,20.7033467163423));
#192935=CARTESIAN_POINT('Ctrl Pts',(18.9000657760964,21.3227304251408,20.6989701589556));
#192936=CARTESIAN_POINT('Ctrl Pts',(18.8272622458552,21.3272006333429,20.6945936015689));
#192937=CARTESIAN_POINT('Ctrl Pts',(18.7543686581099,21.3279020094862,20.6902170441822));
#192938=CARTESIAN_POINT('Ctrl Pts',(18.6815212945107,21.3286029408646,20.6858432621099));
#192939=CARTESIAN_POINT('Ctrl Pts',(18.6085844678842,21.3255397774992,20.6814694800377));
#192940=CARTESIAN_POINT('Ctrl Pts',(18.5359759923093,21.318718077063,20.6770956979654));
#192941=CARTESIAN_POINT('Ctrl Pts',(18.4633896081417,21.3118984521553,20.6727232466332));
#192942=CARTESIAN_POINT('Ctrl Pts',(18.3911318566611,21.3013226055695,20.6683507953009));
#192943=CARTESIAN_POINT('Ctrl Pts',(18.3196168457075,21.2870480730076,20.6639783439686));
#192944=CARTESIAN_POINT('Ctrl Pts',(18.2481000028579,21.2727731747958,20.6596057806336));
#192945=CARTESIAN_POINT('Ctrl Pts',(18.1773264109616,21.2547994988843,20.6552332172986));
#192946=CARTESIAN_POINT('Ctrl Pts',(18.1076997199475,21.2332356339473,20.6508606539636));
#192947=CARTESIAN_POINT('Ctrl Pts',(18.0380007641851,21.2116493881209,20.646483552395));
#192948=CARTESIAN_POINT('Ctrl Pts',(17.9694515476975,21.1864656566405,20.6421064508264));
#192949=CARTESIAN_POINT('Ctrl Pts',(17.9024394813628,21.1578425986309,20.6377293492578));
#192950=CARTESIAN_POINT('Ctrl Pts',(17.8353908150804,21.1292039075796,20.6333498570497));
#192951=CARTESIAN_POINT('Ctrl Pts',(17.7698814039915,21.0971223623162,20.6289703648416));
#192952=CARTESIAN_POINT('Ctrl Pts',(17.706275157963,21.0618027039801,20.6245908726336));
#192953=CARTESIAN_POINT('Ctrl Pts',(17.6425561688916,21.0264204410099,20.6202036177087));
#192954=CARTESIAN_POINT('Ctrl Pts',(17.5807474908118,20.9877888590985,20.6158163627838));
#192955=CARTESIAN_POINT('Ctrl Pts',(17.5211845892524,20.9461564135412,20.6114291078589));
#192956=CARTESIAN_POINT('Ctrl Pts',(17.4806889418755,20.9178513311731,20.60844629937));
#192957=CARTESIAN_POINT('Ctrl Pts',(17.4412307372919,20.8881600257597,20.6054634908812));
#192958=CARTESIAN_POINT('Ctrl Pts',(17.4029060721845,20.8571706944702,20.6024806823924));
#192959=CARTESIAN_POINT('Ctrl Pts',(17.3472665724937,20.8121805847363,20.5981502604166));
#192960=CARTESIAN_POINT('Ctrl Pts',(17.2937883055549,20.764267267587,20.5938198384409));
#192961=CARTESIAN_POINT('Ctrl Pts',(17.2428007358364,20.7136688772175,20.5894894164652));
#192962=CARTESIAN_POINT('Ctrl Pts',(17.1918849324429,20.6631417053928,20.5851650896706));
#192963=CARTESIAN_POINT('Ctrl Pts',(17.1434532240215,20.6099373000743,20.580840762876));
#192964=CARTESIAN_POINT('Ctrl Pts',(17.0978028464019,20.5543346100498,20.5765164360814));
#192965=CARTESIAN_POINT('Ctrl Pts',(17.0522038395386,20.4987944902028,20.5721969754883));
#192966=CARTESIAN_POINT('Ctrl Pts',(17.009380264264,20.4408618239644,20.5678775148952));
#192967=CARTESIAN_POINT('Ctrl Pts',(16.9695918503724,20.3808516493675,20.5635580543021));
#192968=CARTESIAN_POINT('Ctrl Pts',(16.9298290256535,20.3208800691895,20.5592413716891));
#192969=CARTESIAN_POINT('Ctrl Pts',(16.8930977626164,20.2588340443183,20.5549246890762));
#192970=CARTESIAN_POINT('Ctrl Pts',(16.8596158552161,20.1950594889451,20.5506080064632));
#192971=CARTESIAN_POINT('Ctrl Pts',(16.826139467696,20.1312954475459,20.5462920355053));
#192972=CARTESIAN_POINT('Ctrl Pts',(16.7959116071781,20.0658038781863,20.5419760645475));
#192973=CARTESIAN_POINT('Ctrl Pts',(16.7691044221986,19.9989558162336,20.5376600935896));
#192974=CARTESIAN_POINT('Ctrl Pts',(16.7608869589861,19.9784642394291,20.5363370776669));
#192975=CARTESIAN_POINT('Ctrl Pts',(16.752990588142,19.9578453517266,20.5350140617441));
#192976=CARTESIAN_POINT('Ctrl Pts',(16.7454193623258,19.9371102171621,20.5336910458214));
#192977=CARTESIAN_POINT('Ctrl Pts',(16.7454193623258,19.9371102171621,21.3335535344094));
#192978=CARTESIAN_POINT('Ctrl Pts',(16.7201109592649,19.8677987006626,21.3291191840504));
#192979=CARTESIAN_POINT('Ctrl Pts',(16.6984027907146,19.7970869511725,21.3246848336914));
#192980=CARTESIAN_POINT('Ctrl Pts',(16.6804408812102,19.7253772405883,21.3202504833324));
#192981=CARTESIAN_POINT('Ctrl Pts',(16.6624933564997,19.6537249587208,21.3158196842226));
#192982=CARTESIAN_POINT('Ctrl Pts',(16.6482862433426,19.5810767527722,21.3113888851128));
#192983=CARTESIAN_POINT('Ctrl Pts',(16.6379158001016,19.5078501759078,21.306958086003));
#192984=CARTESIAN_POINT('Ctrl Pts',(16.6275504545434,19.434659594212,21.3025294648915));
#192985=CARTESIAN_POINT('Ctrl Pts',(16.6210180961611,19.3608916660175,21.29810084378));
#192986=CARTESIAN_POINT('Ctrl Pts',(16.6183636592833,19.2869728493529,21.2936722226685));
#192987=CARTESIAN_POINT('Ctrl Pts',(16.6174414210567,19.2612910337636,21.2921335747865));
#192988=CARTESIAN_POINT('Ctrl Pts',(16.6169868263632,19.2355910567946,21.2905949269045));
#192989=CARTESIAN_POINT('Ctrl Pts',(16.6170002905214,19.2098909158485,21.2890562790225));
#192990=CARTESIAN_POINT('Origin',(-18.734,19.211,0.));
#192991=CARTESIAN_POINT('',(-20.7225806064498,19.9371103026755,0.755484067882562));
#192992=CARTESIAN_POINT('',(-20.7225806064217,19.9371103027527,0.534177455193947));
#192993=CARTESIAN_POINT('',(-20.7225806064498,19.9371103026755,0.));
#192994=CARTESIAN_POINT('',(-20.8509997094734,19.2121090940372,0.710943721022757));
#192995=CARTESIAN_POINT('Ctrl Pts',(-20.8509997094734,19.2121090940372,
0.710943721022757));
#192996=CARTESIAN_POINT('Ctrl Pts',(-20.8509573780607,19.2929098065566,
0.715781198363344));
#192997=CARTESIAN_POINT('Ctrl Pts',(-20.8462849630088,19.3735486530339,
0.720618675703931));
#192998=CARTESIAN_POINT('Ctrl Pts',(-20.8370625189587,19.4535222491878,
0.725456153044519));
#192999=CARTESIAN_POINT('Ctrl Pts',(-20.827521362655,19.5362595991716,0.730460805517526));
#193000=CARTESIAN_POINT('Ctrl Pts',(-20.8131101367243,19.6182845242239,
0.735465457990533));
#193001=CARTESIAN_POINT('Ctrl Pts',(-20.7939728312899,19.6990583308864,
0.74047011046354));
#193002=CARTESIAN_POINT('Ctrl Pts',(-20.7748355258554,19.7798321375489,
0.745474762936547));
#193003=CARTESIAN_POINT('Ctrl Pts',(-20.7509723452674,19.859354538864,0.750479415409554));
#193004=CARTESIAN_POINT('Ctrl Pts',(-20.7225806064499,19.9371103026755,
0.755484067882561));
#193005=CARTESIAN_POINT('',(-20.3539402423909,20.5738949376539,2.19221145944165E-7));
#193006=CARTESIAN_POINT('Ctrl Pts',(-20.3539402423909,20.5738949376539,
2.19221145944165E-7));
#193007=CARTESIAN_POINT('Ctrl Pts',(-20.307293457224,20.6293394201171,0.00438523054252758));
#193008=CARTESIAN_POINT('Ctrl Pts',(-20.2577052453278,20.6824952398002,
0.00877024186390921));
#193009=CARTESIAN_POINT('Ctrl Pts',(-20.2054289850318,20.7330334234203,
0.0131552531852908));
#193010=CARTESIAN_POINT('Ctrl Pts',(-20.1532303457041,20.7834965668073,
0.0175337535431212));
#193011=CARTESIAN_POINT('Ctrl Pts',(-20.0983519254293,20.8313494565077,
0.0219122539009516));
#193012=CARTESIAN_POINT('Ctrl Pts',(-20.0410868627425,20.8762966502236,
0.026290754258782));
#193013=CARTESIAN_POINT('Ctrl Pts',(-19.9838891952345,20.9211909456449,
0.030664101565157));
#193014=CARTESIAN_POINT('Ctrl Pts',(-19.9243108432097,20.963186041445,0.035037448871532));
#193015=CARTESIAN_POINT('Ctrl Pts',(-19.8626799780617,21.0020249878554,
0.039410796177907));
#193016=CARTESIAN_POINT('Ctrl Pts',(-19.8010881104921,21.040839358514,0.0437813762027675));
#193017=CARTESIAN_POINT('Ctrl Pts',(-19.7374467144134,21.0765012852423,
0.0481519562276279));
#193018=CARTESIAN_POINT('Ctrl Pts',(-19.6721138966915,21.1087964371434,
0.0525225362524884));
#193019=CARTESIAN_POINT('Ctrl Pts',(-19.6068007822918,21.1410818493485,
0.0568917981810319));
#193020=CARTESIAN_POINT('Ctrl Pts',(-19.5397976918714,21.1700022886331,
0.0612610601095754));
#193021=CARTESIAN_POINT('Ctrl Pts',(-19.47148685249,21.1953896145678,0.0656303220381189));
#193022=CARTESIAN_POINT('Ctrl Pts',(-19.4031739921599,21.2207776915762,
0.0699997132295205));
#193023=CARTESIAN_POINT('Ctrl Pts',(-19.3335537597038,21.2426322814668,
0.0743691044209222));
#193024=CARTESIAN_POINT('Ctrl Pts',(-19.2630262593487,21.2608341925433,
0.0787384956123238));
#193025=CARTESIAN_POINT('Ctrl Pts',(-19.1924269638886,21.2790546326773,
0.0831123347268408));
#193026=CARTESIAN_POINT('Ctrl Pts',(-19.1209190256057,21.2936148503494,
0.0874861738413579));
#193027=CARTESIAN_POINT('Ctrl Pts',(-19.048914683673,21.3044463790618,0.0918600129558749));
#193028=CARTESIAN_POINT('Ctrl Pts',(-18.9768705191299,21.3152838982429,
0.0962362710591149));
#193029=CARTESIAN_POINT('Ctrl Pts',(-18.9043298854534,21.3223885760892,
0.100612529162355));
#193030=CARTESIAN_POINT('Ctrl Pts',(-18.8317094286013,21.3257439248198,
0.104988787265595));
#193031=CARTESIAN_POINT('Ctrl Pts',(-18.7589648320255,21.3291050092906,
0.109372526283929));
#193032=CARTESIAN_POINT('Ctrl Pts',(-18.6861406230801,21.3287039714963,
0.113756265302264));
#193033=CARTESIAN_POINT('Ctrl Pts',(-18.6136520423459,21.324576440323,0.118140004320598));
#193034=CARTESIAN_POINT('Ctrl Pts',(-18.5716442693831,21.3221844995419,
0.1206804198115));
#193035=CARTESIAN_POINT('Ctrl Pts',(-18.5297491060651,21.3185420587999,
0.123220835302401));
#193036=CARTESIAN_POINT('Ctrl Pts',(-18.4880458562809,21.3136639196951,
0.125761250793303));
#193037=CARTESIAN_POINT('Ctrl Pts',(-18.415885212538,21.3052230988983,0.13015702374017));
#193038=CARTESIAN_POINT('Ctrl Pts',(-18.3440242467257,21.2930474771355,
0.134552796687038));
#193039=CARTESIAN_POINT('Ctrl Pts',(-18.2728788054798,21.2771694615796,
0.138948569633906));
#193040=CARTESIAN_POINT('Ctrl Pts',(-18.201836191067,21.2613143945926,0.143337989349937));
#193041=CARTESIAN_POINT('Ctrl Pts',(-18.1315075132681,21.2417676616992,
0.147727409065968));
#193042=CARTESIAN_POINT('Ctrl Pts',(-18.0623022558513,21.2186132945629,
0.152116828781999));
#193043=CARTESIAN_POINT('Ctrl Pts',(-17.9931750162606,21.1954850302611,
0.156501300131437));
#193044=CARTESIAN_POINT('Ctrl Pts',(-17.9251691345193,21.168757363137,0.160885771480875));
#193045=CARTESIAN_POINT('Ctrl Pts',(-17.8586810464524,21.1385647147529,
0.165270242830314));
#193046=CARTESIAN_POINT('Ctrl Pts',(-17.7922332423912,21.1083903595827,
0.169652057702872));
#193047=CARTESIAN_POINT('Ctrl Pts',(-17.7273018435918,21.0747553873414,
0.17403387257543));
#193048=CARTESIAN_POINT('Ctrl Pts',(-17.6642640090405,21.0378426066976,
0.178415687447987));
#193049=CARTESIAN_POINT('Ctrl Pts',(-17.6012437811927,21.0009401359319,
0.182796278463219));
#193050=CARTESIAN_POINT('Ctrl Pts',(-17.5401164818004,20.9607619172419,
0.187176869478451));
#193051=CARTESIAN_POINT('Ctrl Pts',(-17.4812338530683,20.9175362525015,
0.191557460493683));
#193052=CARTESIAN_POINT('Ctrl Pts',(-17.4223484413191,20.8743085447517,
0.195938258552312));
#193053=CARTESIAN_POINT('Ctrl Pts',(-17.3657082969835,20.8280333908516,
0.20031905661094));
#193054=CARTESIAN_POINT('Ctrl Pts',(-17.3116340465775,20.7789808973787,
0.204699854669569));
#193055=CARTESIAN_POINT('Ctrl Pts',(-17.2575026772116,20.7298765894583,
0.209085280191852));
#193056=CARTESIAN_POINT('Ctrl Pts',(-17.2059429696119,20.6779894082537,
0.213470705714135));
#193057=CARTESIAN_POINT('Ctrl Pts',(-17.157239849178,20.6236274904517,0.217856131236418));
#193058=CARTESIAN_POINT('Ctrl Pts',(-17.1085094838156,20.569235162143,0.222244010002027));
#193059=CARTESIAN_POINT('Ctrl Pts',(-17.0626391892086,20.5123657149587,
0.226631888767637));
#193060=CARTESIAN_POINT('Ctrl Pts',(-17.0198728898628,20.4533595495237,
0.231019767533247));
#193061=CARTESIAN_POINT('Ctrl Pts',(-16.9770308541579,20.3942488879738,
0.235415416949269));
#193062=CARTESIAN_POINT('Ctrl Pts',(-16.9373040526505,20.3329943550553,
0.23981106636529));
#193063=CARTESIAN_POINT('Ctrl Pts',(-16.9008921528455,20.2699639373937,
0.244206715781312));
#193064=CARTESIAN_POINT('Ctrl Pts',(-16.876785868281,20.2282350193065,0.247116829679121));
#193065=CARTESIAN_POINT('Ctrl Pts',(-16.8541315650652,20.1857282478032,
0.250026943576929));
#193066=CARTESIAN_POINT('Ctrl Pts',(-16.8329755574333,20.1425551882545,
0.252937057474737));
#193067=CARTESIAN_POINT('Ctrl Pts',(-16.8011149178839,20.077537188996,0.257319646645566));
#193068=CARTESIAN_POINT('Ctrl Pts',(-16.7725299917263,20.0107527148536,
0.261702235816396));
#193069=CARTESIAN_POINT('Ctrl Pts',(-16.7474198406578,19.9425656296656,
0.266084824987225));
#193070=CARTESIAN_POINT('Ctrl Pts',(-16.7223474688912,19.8744811348787,
0.270460820364237));
#193071=CARTESIAN_POINT('Ctrl Pts',(-16.7007396607462,19.8049986679621,
0.27483681574125));
#193072=CARTESIAN_POINT('Ctrl Pts',(-16.6827487993224,19.7345050254953,
0.279212811118263));
#193073=CARTESIAN_POINT('Ctrl Pts',(-16.6647794915184,19.6640958366371,
0.2835835639147));
#193074=CARTESIAN_POINT('Ctrl Pts',(-16.6504186420449,19.5926783449244,
0.287954316711137));
#193075=CARTESIAN_POINT('Ctrl Pts',(-16.6397693071744,19.5206559465392,
0.292325069507573));
#193076=CARTESIAN_POINT('Ctrl Pts',(-16.6291268685744,19.4486801882447,
0.296692991902476));
#193077=CARTESIAN_POINT('Ctrl Pts',(-16.6221912467961,19.3761007777964,
0.30106091429738));
#193078=CARTESIAN_POINT('Ctrl Pts',(-16.6190144407725,19.3033313828499,
0.305428836692283));
#193079=CARTESIAN_POINT('Ctrl Pts',(-16.6158386365901,19.2305849365468,
0.309795381613953));
#193080=CARTESIAN_POINT('Ctrl Pts',(-16.6164193161497,19.1576491077124,
0.314161926535623));
#193081=CARTESIAN_POINT('Ctrl Pts',(-16.6207564869952,19.0849410663897,
0.318528471457294));
#193082=CARTESIAN_POINT('Ctrl Pts',(-16.6250937309155,19.0122318000446,
0.322895089948759));
#193083=CARTESIAN_POINT('Ctrl Pts',(-16.6331875609615,18.9397508116577,
0.327261708440224));
#193084=CARTESIAN_POINT('Ctrl Pts',(-16.6449859783168,18.867911939568,0.33162832693169));
#193085=CARTESIAN_POINT('Ctrl Pts',(-16.6567966078099,18.7959987095218,
0.335999465160437));
#193086=CARTESIAN_POINT('Ctrl Pts',(-16.6723194019262,18.7247294012091,
0.340370603389185));
#193087=CARTESIAN_POINT('Ctrl Pts',(-16.6914510303897,18.6545085744202,
0.344741741617932));
#193088=CARTESIAN_POINT('Ctrl Pts',(-16.7105930357156,18.5842496603426,
0.349115250721684));
#193089=CARTESIAN_POINT('Ctrl Pts',(-16.7333476210311,18.5150408198693,
0.353488759825437));
#193090=CARTESIAN_POINT('Ctrl Pts',(-16.7595620940046,18.447269710324,0.357862268929189));
#193091=CARTESIAN_POINT('Ctrl Pts',(-16.7858233028863,18.3793777765168,
0.362243575249379));
#193092=CARTESIAN_POINT('Ctrl Pts',(-16.8155565194801,18.3129291342219,
0.366624881569569));
#193093=CARTESIAN_POINT('Ctrl Pts',(-16.8485618556777,18.2482892418101,
0.371006187889759));
#193094=CARTESIAN_POINT('Ctrl Pts',(-16.8714293819244,18.2035039250522,
0.37404174664523));
#193095=CARTESIAN_POINT('Ctrl Pts',(-16.8958666541819,18.1595863577281,
0.3770773054007));
#193096=CARTESIAN_POINT('Ctrl Pts',(-16.9217951530525,18.1166496937908,
0.380112864156171));
#193097=CARTESIAN_POINT('Ctrl Pts',(-16.9592870771133,18.0545644125798,
0.384502201884909));
#193098=CARTESIAN_POINT('Ctrl Pts',(-17.000046146169,17.9942872611045,0.388891539613646));
#193099=CARTESIAN_POINT('Ctrl Pts',(-17.0438725732189,17.9361830401024,
0.393280877342384));
#193100=CARTESIAN_POINT('Ctrl Pts',(-17.0876340137246,17.8781649769917,
0.397663706489195));
#193101=CARTESIAN_POINT('Ctrl Pts',(-17.1344534950993,17.8223138297407,
0.402046535636006));
#193102=CARTESIAN_POINT('Ctrl Pts',(-17.184086764136,17.7689674201692,0.406429364782818));
#193103=CARTESIAN_POINT('Ctrl Pts',(-17.2336617334565,17.7156836718045,
0.410807045816273));
#193104=CARTESIAN_POINT('Ctrl Pts',(-17.2860435979522,17.6648991677451,
0.415184726849729));
#193105=CARTESIAN_POINT('Ctrl Pts',(-17.3409475304283,17.616919130966,0.419562407883185));
#193106=CARTESIAN_POINT('Ctrl Pts',(-17.3958166506481,17.5689695162945,
0.423937313214657));
#193107=CARTESIAN_POINT('Ctrl Pts',(-17.4532043037707,17.5238211571201,
0.428312218546129));
#193108=CARTESIAN_POINT('Ctrl Pts',(-17.512789475476,17.4817418195099,0.4326871238776));
#193109=CARTESIAN_POINT('Ctrl Pts',(-17.5723564947758,17.4396753012166,
0.4370606964101));
#193110=CARTESIAN_POINT('Ctrl Pts',(-17.6341193099785,17.4006762261876,
0.4414342689426));
#193111=CARTESIAN_POINT('Ctrl Pts',(-17.6977258981411,17.3649704807841,
0.445807841475099));
#193112=CARTESIAN_POINT('Ctrl Pts',(-17.7613340609317,17.3292638514585,
0.450181522278617));
#193113=CARTESIAN_POINT('Ctrl Pts',(-17.8267856659412,17.29685094787,0.454555203082135));
#193114=CARTESIAN_POINT('Ctrl Pts',(-17.8937034068913,17.2679120875241,
0.458928883885652));
#193115=CARTESIAN_POINT('Ctrl Pts',(-17.9606903750842,17.238943289564,0.463307089316848));
#193116=CARTESIAN_POINT('Ctrl Pts',(-18.0291460640642,17.2134559021899,
0.467685294748045));
#193117=CARTESIAN_POINT('Ctrl Pts',(-18.0986732370017,17.191582038255,0.472063500179241));
#193118=CARTESIAN_POINT('Ctrl Pts',(-18.1682382801082,17.1696962600299,
0.476444090338191));
#193119=CARTESIAN_POINT('Ctrl Pts',(-18.2388755021192,17.1514280448653,
0.48082468049714));
#193120=CARTESIAN_POINT('Ctrl Pts',(-18.3101751880181,17.1368588455102,
0.48520527065609));
#193121=CARTESIAN_POINT('Ctrl Pts',(-18.3816008664645,17.1222639011532,
0.489593601686642));
#193122=CARTESIAN_POINT('Ctrl Pts',(-18.4536908693965,17.1113810977932,
0.493981932717194));
#193123=CARTESIAN_POINT('Ctrl Pts',(-18.5260286230796,17.1042401877808,
0.498370263747746));
#193124=CARTESIAN_POINT('Ctrl Pts',(-18.5750326393233,17.0994026962577,
0.501343066111033));
#193125=CARTESIAN_POINT('Ctrl Pts',(-18.624150260615,17.0962813311373,0.504315868474319));
#193126=CARTESIAN_POINT('Ctrl Pts',(-18.6732524681258,17.0948717578154,
0.507288670837606));
#193127=CARTESIAN_POINT('Ctrl Pts',(-18.7457477325718,17.0927906417942,
0.511677762579041));
#193128=CARTESIAN_POINT('Ctrl Pts',(-18.818490899314,17.0944351534906,0.516066854320476));
#193129=CARTESIAN_POINT('Ctrl Pts',(-18.8910671105736,17.0998347002719,
0.520455946061912));
#193130=CARTESIAN_POINT('Ctrl Pts',(-18.9635359557305,17.1052262591976,
0.524838544771176));
#193131=CARTESIAN_POINT('Ctrl Pts',(-19.035837858837,17.1143617900503,0.52922114348044));
#193132=CARTESIAN_POINT('Ctrl Pts',(-19.1075565880863,17.1272187073742,
0.533603742189705));
#193133=CARTESIAN_POINT('Ctrl Pts',(-19.1791914726444,17.1400605939763,
0.537981217305188));
#193134=CARTESIAN_POINT('Ctrl Pts',(-19.2502440654555,17.1566151398615,
0.542358692420671));
#193135=CARTESIAN_POINT('Ctrl Pts',(-19.320303591177,17.1768079984984,0.546736167536153));
#193136=CARTESIAN_POINT('Ctrl Pts',(-19.3903189366747,17.1969881233207,
0.551110882172916));
#193137=CARTESIAN_POINT('Ctrl Pts',(-19.4593419954754,17.2208018753163,
0.555485596809679));
#193138=CARTESIAN_POINT('Ctrl Pts',(-19.5269739113633,17.2481242077255,
0.559860311446443));
#193139=CARTESIAN_POINT('Ctrl Pts',(-19.5945854628883,17.2754383132217,
0.564233708831213));
#193140=CARTESIAN_POINT('Ctrl Pts',(-19.6608062563391,17.3062587212116,
0.568607106215984));
#193141=CARTESIAN_POINT('Ctrl Pts',(-19.7252558767888,17.3404116469058,
0.572980503600755));
#193142=CARTESIAN_POINT('Ctrl Pts',(-19.7897073269136,17.3745655421752,
0.577354025142908));
#193143=CARTESIAN_POINT('Ctrl Pts',(-19.8523870791113,17.4120519154596,
0.581727546685062));
#193144=CARTESIAN_POINT('Ctrl Pts',(-19.9129393606855,17.4526510631202,
0.586101068227215));
#193145=CARTESIAN_POINT('Ctrl Pts',(-19.9735546434687,17.4932924518874,
0.590479140170077));
#193146=CARTESIAN_POINT('Ctrl Pts',(-20.0320376349006,17.537052812133,0.594857212112939));
#193147=CARTESIAN_POINT('Ctrl Pts',(-20.0880623158585,17.5836695956961,
0.599235284055801));
#193148=CARTESIAN_POINT('Ctrl Pts',(-20.1441176953744,17.6303119227877,
0.603615754950226));
#193149=CARTESIAN_POINT('Ctrl Pts',(-20.1977117280627,17.6798134620822,
0.607996225844651));
#193150=CARTESIAN_POINT('Ctrl Pts',(-20.2485542488444,17.7318737622139,
0.612376696739076));
#193151=CARTESIAN_POINT('Ctrl Pts',(-20.2994868988123,17.7840263503048,
0.616764932950222));
#193152=CARTESIAN_POINT('Ctrl Pts',(-20.3476579775569,17.8387463951232,
0.621153169161368));
#193153=CARTESIAN_POINT('Ctrl Pts',(-20.3928170879059,17.8956997039188,
0.625541405372514));
#193154=CARTESIAN_POINT('Ctrl Pts',(-20.4234260448481,17.9343027978054,
0.628515762754689));
#193155=CARTESIAN_POINT('Ctrl Pts',(-20.4526521208593,17.9739312228937,
0.631490120136864));
#193156=CARTESIAN_POINT('Ctrl Pts',(-20.4804290546179,18.0144739630136,
0.634464477519039));
#193157=CARTESIAN_POINT('Ctrl Pts',(-20.5219871907903,18.0751315118038,
0.638914527700529));
#193158=CARTESIAN_POINT('Ctrl Pts',(-20.5604590132257,18.1380695894107,
0.643364577882019));
#193159=CARTESIAN_POINT('Ctrl Pts',(-20.5955899392305,18.2029464805101,
0.647814628063508));
#193160=CARTESIAN_POINT('Ctrl Pts',(-20.6306645724414,18.2677194147297,
0.652257547611509));
#193161=CARTESIAN_POINT('Ctrl Pts',(-20.6624087216052,18.3344245877164,
0.65670046715951));
#193162=CARTESIAN_POINT('Ctrl Pts',(-20.6906107187659,18.4026909655271,
0.661143386707512));
#193163=CARTESIAN_POINT('Ctrl Pts',(-20.7187694104787,18.4708525172134,
0.665579483950703));
#193164=CARTESIAN_POINT('Ctrl Pts',(-20.7433965899229,18.5405700796876,
0.670015581193894));
#193165=CARTESIAN_POINT('Ctrl Pts',(-20.7643270288141,18.6114492047649,
0.674451678437085));
#193166=CARTESIAN_POINT('Ctrl Pts',(-20.7852384786614,18.6822640250841,
0.678883751051583));
#193167=CARTESIAN_POINT('Ctrl Pts',(-20.8024597179405,18.7542378712037,
0.68331582366608));
#193168=CARTESIAN_POINT('Ctrl Pts',(-20.8158744295843,18.8269585185907,
0.687747896280578));
#193169=CARTESIAN_POINT('Ctrl Pts',(-20.8292815989961,18.8996382798217,
0.692177477024898));
#193170=CARTESIAN_POINT('Ctrl Pts',(-20.8388864061313,18.9730635524855,
0.696607057769218));
#193171=CARTESIAN_POINT('Ctrl Pts',(-20.8446233280938,19.0468105761441,
0.701036638513538));
#193172=CARTESIAN_POINT('Ctrl Pts',(-20.8489003437794,19.1017907866147,
0.704338999334862));
#193173=CARTESIAN_POINT('Ctrl Pts',(-20.851028607491,19.156949536228,0.707641360156185));
#193174=CARTESIAN_POINT('Ctrl Pts',(-20.8509997094738,19.2121090932814,
0.710943720977509));
#193175=CARTESIAN_POINT('',(-17.1140743056112,20.5739122292573,0.));
#193176=CARTESIAN_POINT('Origin',(-18.734,19.211,0.));
#193177=CARTESIAN_POINT('',(-20.8509993841467,19.2126147825168,0.48905627896718));
#193178=CARTESIAN_POINT('Ctrl Pts',(-20.8509993841467,19.2126147825168,
0.48905627896718));
#193179=CARTESIAN_POINT('Ctrl Pts',(-20.8510560155281,19.1383703573979,
0.484575909845393));
#193180=CARTESIAN_POINT('Ctrl Pts',(-20.8472020813435,19.0639814494018,
0.480095540723607));
#193181=CARTESIAN_POINT('Ctrl Pts',(-20.8394225379869,18.9899006184163,
0.47561517160182));
#193182=CARTESIAN_POINT('Ctrl Pts',(-20.8319236734385,18.9184925560489,
0.471296450099625));
#193183=CARTESIAN_POINT('Ctrl Pts',(-20.8207776608864,18.8473712681642,
0.466977728597429));
#193184=CARTESIAN_POINT('Ctrl Pts',(-20.806023944847,18.7769426627958,0.462659007095234));
#193185=CARTESIAN_POINT('Ctrl Pts',(-20.791280057372,18.7065609752404,0.458343162619601));
#193186=CARTESIAN_POINT('Ctrl Pts',(-20.7729333325562,18.6368715401201,
0.454027318143968));
#193187=CARTESIAN_POINT('Ctrl Pts',(-20.7510747141467,18.5682725324448,
0.449711473668335));
#193188=CARTESIAN_POINT('Ctrl Pts',(-20.7292229865185,18.4996951501417,
0.445396989733422));
#193189=CARTESIAN_POINT('Ctrl Pts',(-20.7038617126699,18.4322079861377,
0.441082505798508));
#193190=CARTESIAN_POINT('Ctrl Pts',(-20.6751318568351,18.3661946292903,
0.436768021863595));
#193191=CARTESIAN_POINT('Ctrl Pts',(-20.6464009762914,18.3001789179419,
0.432453384043816));
#193192=CARTESIAN_POINT('Ctrl Pts',(-20.6143014765397,18.2356375721218,
0.428138746224037));
#193193=CARTESIAN_POINT('Ctrl Pts',(-20.5790219308427,18.1729330104904,
0.423824108404258));
#193194=CARTESIAN_POINT('Ctrl Pts',(-20.5437074960946,18.1101664383482,
0.419505203703596));
#193195=CARTESIAN_POINT('Ctrl Pts',(-20.5052069868332,18.0492407068168,
0.415186299002933));
#193196=CARTESIAN_POINT('Ctrl Pts',(-20.4637537219139,17.9904914742105,
0.410867394302271));
#193197=CARTESIAN_POINT('Ctrl Pts',(-20.4222758014217,17.9317072987355,
0.406545920803466));
#193198=CARTESIAN_POINT('Ctrl Pts',(-20.377841940606,17.8751025856419,0.402224447304661));
#193199=CARTESIAN_POINT('Ctrl Pts',(-20.3307256272438,17.8209797586716,
0.397902973805856));
#193200=CARTESIAN_POINT('Ctrl Pts',(-20.2835347249498,17.7667712508921,
0.393574659065255));
#193201=CARTESIAN_POINT('Ctrl Pts',(-20.233653247686,17.7150528185668,0.389246344324653));
#193202=CARTESIAN_POINT('Ctrl Pts',(-20.1813905470417,17.6660891273817,
0.384918029584051));
#193203=CARTESIAN_POINT('Ctrl Pts',(-20.1677437875061,17.6533038003446,
0.383787826404133));
#193204=CARTESIAN_POINT('Ctrl Pts',(-20.1539348347408,17.6407060782365,
0.382657623224215));
#193205=CARTESIAN_POINT('Ctrl Pts',(-20.139969531998,17.6283001942588,0.381527420044297));
#193206=CARTESIAN_POINT('Ctrl Pts',(-20.0856806361701,17.5800734028086,
0.377133853801673));
#193207=CARTESIAN_POINT('Ctrl Pts',(-20.028804456646,17.534551575879,0.372740287559048));
#193208=CARTESIAN_POINT('Ctrl Pts',(-19.9696413059749,17.4920236874905,
0.368346721316423));
#193209=CARTESIAN_POINT('Ctrl Pts',(-19.9105644543722,17.4495578329374,
0.363959563804056));
#193210=CARTESIAN_POINT('Ctrl Pts',(-19.8492076419245,17.410077525157,0.359572406291689));
#193211=CARTESIAN_POINT('Ctrl Pts',(-19.7859055363077,17.3738326851685,
0.355185248779322));
#193212=CARTESIAN_POINT('Ctrl Pts',(-19.7226758978492,17.3376293376474,
0.350803113609178));
#193213=CARTESIAN_POINT('Ctrl Pts',(-19.6575058056516,17.3046543374869,
0.346420978439034));
#193214=CARTESIAN_POINT('Ctrl Pts',(-19.5907589079216,17.2751143696755,
0.342038843268889));
#193215=CARTESIAN_POINT('Ctrl Pts',(-19.52405315142,17.2455926096101,0.337659409144484));
#193216=CARTESIAN_POINT('Ctrl Pts',(-19.4557729567064,17.219501874687,0.333279975020079));
#193217=CARTESIAN_POINT('Ctrl Pts',(-19.3863053176005,17.1970022908081,
0.328900540895673));
#193218=CARTESIAN_POINT('Ctrl Pts',(-19.3168577535507,17.1745092089554,
0.324522372358903));
#193219=CARTESIAN_POINT('Ctrl Pts',(-19.2462238836977,17.1556053656812,
0.320144203822133));
#193220=CARTESIAN_POINT('Ctrl Pts',(-19.1748077989579,17.1404016602977,
0.315766035285362));
#193221=CARTESIAN_POINT('Ctrl Pts',(-19.1033889720518,17.1251973711369,
0.31138769863987));
#193222=CARTESIAN_POINT('Ctrl Pts',(-19.0311883413905,17.1136936001516,
0.307009361994378));
#193223=CARTESIAN_POINT('Ctrl Pts',(-18.9586205452229,17.1059502118326,
0.302631025348886));
#193224=CARTESIAN_POINT('Ctrl Pts',(-18.8859767969382,17.0981987189993,
0.298248106175672));
#193225=CARTESIAN_POINT('Ctrl Pts',(-18.8129655950943,17.0942155178377,
0.293865187002457));
#193226=CARTESIAN_POINT('Ctrl Pts',(-18.7400062483051,17.0940085203333,
0.289482267829242));
#193227=CARTESIAN_POINT('Ctrl Pts',(-18.667006546944,17.0938014083365,0.285096924417947));
#193228=CARTESIAN_POINT('Ctrl Pts',(-18.5940592383891,17.0973746352134,
0.280711581006652));
#193229=CARTESIAN_POINT('Ctrl Pts',(-18.5215804684088,17.1046840354309,
0.276326237595358));
#193230=CARTESIAN_POINT('Ctrl Pts',(-18.4489736078897,17.1120063534313,
0.27193314403874));
#193231=CARTESIAN_POINT('Ctrl Pts',(-18.3768374152679,17.1230779575914,
0.267540050482122));
#193232=CARTESIAN_POINT('Ctrl Pts',(-18.3055792094826,17.1378032832718,
0.263146956925504));
#193233=CARTESIAN_POINT('Ctrl Pts',(-18.2580242315412,17.1476303976399,
0.260215175737957));
#193234=CARTESIAN_POINT('Ctrl Pts',(-18.2108600441032,17.159083715391,0.257283394550411));
#193235=CARTESIAN_POINT('Ctrl Pts',(-18.1642034381997,17.1721226426878,
0.254351613362864));
#193236=CARTESIAN_POINT('Ctrl Pts',(-18.0951058972849,17.1914330446111,
0.250009701502008));
#193237=CARTESIAN_POINT('Ctrl Pts',(-18.0268399854881,17.2143024101294,
0.245667789641151));
#193238=CARTESIAN_POINT('Ctrl Pts',(-17.9598043906284,17.2406421242755,
0.241325877780295));
#193239=CARTESIAN_POINT('Ctrl Pts',(-17.8928697395248,17.266942175468,0.236990504071199));
#193240=CARTESIAN_POINT('Ctrl Pts',(-17.8271621848896,17.29670202984,0.232655130362104));
#193241=CARTESIAN_POINT('Ctrl Pts',(-17.7630669345953,17.3297828454684,
0.228319756653008));
#193242=CARTESIAN_POINT('Ctrl Pts',(-17.6990453506667,17.3628256404409,
0.223989365703531));
#193243=CARTESIAN_POINT('Ctrl Pts',(-17.6366328289127,17.3991815955315,
0.219658974754055));
#193244=CARTESIAN_POINT('Ctrl Pts',(-17.5761945067699,17.4386638468264,
0.215328583804578));
#193245=CARTESIAN_POINT('Ctrl Pts',(-17.5157933283169,17.4781218334421,
0.211000854191369));
#193246=CARTESIAN_POINT('Ctrl Pts',(-17.4573643561353,17.5207020380533,
0.206673124578159));
#193247=CARTESIAN_POINT('Ctrl Pts',(-17.4012466091922,17.5661725320599,
0.20234539496495));
#193248=CARTESIAN_POINT('Ctrl Pts',(-17.3451439091012,17.6116308340625,
0.198018825745928));
#193249=CARTESIAN_POINT('Ctrl Pts',(-17.2913515880727,17.6599775776502,
0.193692256526906));
#193250=CARTESIAN_POINT('Ctrl Pts',(-17.2401767514859,17.7109396338151,
0.189365687307884));
#193251=CARTESIAN_POINT('Ctrl Pts',(-17.1889979072007,17.7619056810148,
0.185038779258574));
#193252=CARTESIAN_POINT('Ctrl Pts',(-17.140437302276,17.8154870975617,0.180711871209265));
#193253=CARTESIAN_POINT('Ctrl Pts',(-17.09476491744,17.8713741775763,0.176384963159955));
#193254=CARTESIAN_POINT('Ctrl Pts',(-17.049037723187,17.9273283252134,0.172052862578918));
#193255=CARTESIAN_POINT('Ctrl Pts',(-17.0062059805784,17.9855932764929,
0.167720761997882));
#193256=CARTESIAN_POINT('Ctrl Pts',(-16.9664985330236,18.0458272384593,
0.163388661416845));
#193257=CARTESIAN_POINT('Ctrl Pts',(-16.9267665792057,18.1060983750469,
0.159053887191356));
#193258=CARTESIAN_POINT('Ctrl Pts',(-16.890163004568,18.1683405133194,0.154719112965868));
#193259=CARTESIAN_POINT('Ctrl Pts',(-16.8568710208892,18.2321865367791,
0.150384338740379));
#193260=CARTESIAN_POINT('Ctrl Pts',(-16.8235119906462,18.2961611394354,
0.146040834734134));
#193261=CARTESIAN_POINT('Ctrl Pts',(-16.7934780711976,18.3617456271073,
0.141697330727888));
#193262=CARTESIAN_POINT('Ctrl Pts',(-16.7669043702655,18.4285526960368,
0.137353826721643));
#193263=CARTESIAN_POINT('Ctrl Pts',(-16.7461478827045,18.4807351187546,
0.133961153374905));
#193264=CARTESIAN_POINT('Ctrl Pts',(-16.7275015133356,18.5336630097783,
0.130568480028167));
#193265=CARTESIAN_POINT('Ctrl Pts',(-16.7110080390405,18.5871470318309,
0.127175806681429));
#193266=CARTESIAN_POINT('Ctrl Pts',(-16.6890808417458,18.6582511959801,
0.122665427818863));
#193267=CARTESIAN_POINT('Ctrl Pts',(-16.6708715522275,18.7306260888239,
0.118155048956298));
#193268=CARTESIAN_POINT('Ctrl Pts',(-16.6565194459451,18.8038593025457,
0.113644670093733));
#193269=CARTESIAN_POINT('Ctrl Pts',(-16.6414519720022,18.8807427590775,
0.108909475506494));
#193270=CARTESIAN_POINT('Ctrl Pts',(-16.6306364414031,18.9585718864235,
0.104174280919254));
#193271=CARTESIAN_POINT('Ctrl Pts',(-16.624175177866,19.0368500074442,0.0994390863320154));
#193272=CARTESIAN_POINT('Ctrl Pts',(-16.6180411415214,19.1111637754199,
0.0949437031101447));
#193273=CARTESIAN_POINT('Ctrl Pts',(-16.6158311470803,19.18588164953,0.090448319888274));
#193274=CARTESIAN_POINT('Ctrl Pts',(-16.6175803959886,19.2605687376906,
0.0859529366664034));
#193275=CARTESIAN_POINT('Ctrl Pts',(-16.6193280001048,19.3351855987192,
0.0814617803849421));
#193276=CARTESIAN_POINT('Ctrl Pts',(-16.6250274372589,19.4097712832384,
0.0769706241034808));
#193277=CARTESIAN_POINT('Ctrl Pts',(-16.6346618981062,19.4838892338239,
0.0724794678220195));
#193278=CARTESIAN_POINT('Ctrl Pts',(-16.6442898170097,19.5579568572063,
0.0679913611032202));
#193279=CARTESIAN_POINT('Ctrl Pts',(-16.6578473889511,19.6315569329051,
0.0635032543844209));
#193280=CARTESIAN_POINT('Ctrl Pts',(-16.6752659458499,19.7042576347942,
0.0590151476656216));
#193281=CARTESIAN_POINT('Ctrl Pts',(-16.6926772219334,19.7769279483805,
0.0545289169389693));
#193282=CARTESIAN_POINT('Ctrl Pts',(-16.7139461674509,19.848699198966,0.0500426862123171));
#193283=CARTESIAN_POINT('Ctrl Pts',(-16.7389532085404,19.9191506194919,
0.0455564554856648));
#193284=CARTESIAN_POINT('Ctrl Pts',(-16.7639633583527,19.9896107981087,
0.0410696670581777));
#193285=CARTESIAN_POINT('Ctrl Pts',(-16.7927123885947,20.0587503922127,
0.0365828786306905));
#193286=CARTESIAN_POINT('Ctrl Pts',(-16.8250314087852,20.1261655138582,
0.0320960902032033));
#193287=CARTESIAN_POINT('Ctrl Pts',(-16.8573519842582,20.1935838797096,
0.0276090858587915));
#193288=CARTESIAN_POINT('Ctrl Pts',(-16.8932426902262,20.2592772053157,
0.0231220815143796));
#193289=CARTESIAN_POINT('Ctrl Pts',(-16.932487950158,20.3228648003575,0.0186350771699677));
#193290=CARTESIAN_POINT('Ctrl Pts',(-16.9717602972259,20.3864962836509,
0.0141449758885641));
#193291=CARTESIAN_POINT('Ctrl Pts',(-17.0143915779344,20.4480187554704,
0.00965487460716038));
#193292=CARTESIAN_POINT('Ctrl Pts',(-17.0601224600125,20.5070798513692,
0.0051647733257567));
#193293=CARTESIAN_POINT('Ctrl Pts',(-17.0776565589201,20.5297250103958,
0.00344318221716946));
#193294=CARTESIAN_POINT('Ctrl Pts',(-17.0956458992255,20.5520086551532,
0.00172159110858221));
#193295=CARTESIAN_POINT('Ctrl Pts',(-17.1140743056112,20.5739122292573,
-5.04250086090388E-15));
#193296=CARTESIAN_POINT('Ctrl Pts',(-20.8509994310879,19.2125520223715,
0.490010528127495));
#193297=CARTESIAN_POINT('Ctrl Pts',(-20.8509485244656,19.2819899972947,
0.494577406431818));
#193298=CARTESIAN_POINT('Ctrl Pts',(-20.8474812586126,19.3513903947451,
0.499099088403655));
#193299=CARTESIAN_POINT('Ctrl Pts',(-20.8382973967345,19.4437375097343,
0.504962354973714));
#193300=CARTESIAN_POINT('Ctrl Pts',(-20.835602110511,19.466935447343,0.506422052247473));
#193301=CARTESIAN_POINT('Ctrl Pts',(-20.8317146529006,19.4961663924751,
0.508240780883106));
#193302=CARTESIAN_POINT('Ctrl Pts',(-20.8308794508201,19.5022442397664,
0.508617812016216));
#193303=CARTESIAN_POINT('Ctrl Pts',(-20.8294395919533,19.5123948705701,
0.509245509884849));
#193304=CARTESIAN_POINT('Ctrl Pts',(-20.8288494591845,19.5164696311213,
0.50949695144284));
#193305=CARTESIAN_POINT('Ctrl Pts',(-20.8277537164569,19.5238830074484,
0.509953403504262));
#193306=CARTESIAN_POINT('Ctrl Pts',(-20.8272520009022,19.5272221728698,
0.510158628848267));
#193307=CARTESIAN_POINT('Ctrl Pts',(-20.8262053588598,19.5340764444855,
0.510579109141992));
#193308=CARTESIAN_POINT('Ctrl Pts',(-20.8256595644637,19.5375913647262,
0.510794307785923));
#193309=CARTESIAN_POINT('Ctrl Pts',(-20.8244066116742,19.5455284026313,
0.51127928381383));
#193310=CARTESIAN_POINT('Ctrl Pts',(-20.8236942817571,19.5499496480936,
0.511548763855699));
#193311=CARTESIAN_POINT('Ctrl Pts',(-20.8214988308291,19.5633062157398,
0.512360924113693));
#193312=CARTESIAN_POINT('Ctrl Pts',(-20.8199723679794,19.5722344461074,
0.512901190399044));
#193313=CARTESIAN_POINT('Ctrl Pts',(-20.8078159804437,19.6406889785574,
0.517025262324955));
#193314=CARTESIAN_POINT('Ctrl Pts',(-20.7946963208786,19.69975090938,0.52047760042993));
#193315=CARTESIAN_POINT('Ctrl Pts',(-20.7741781413724,19.7764374678371,
0.52491533155393));
#193316=CARTESIAN_POINT('Ctrl Pts',(-20.7690474666048,19.7946336297256,
0.525964916091698));
#193317=CARTESIAN_POINT('Ctrl Pts',(-20.7520374606963,19.8520067038969,
0.529270205287377));
#193318=CARTESIAN_POINT('Ctrl Pts',(-20.7392650272457,19.8909096372322,
0.531505467687245));
#193319=CARTESIAN_POINT('Ctrl Pts',(-20.724446703344,19.9319843000659,0.533880820955069));
#193320=CARTESIAN_POINT('Ctrl Pts',(-20.7235161259709,19.9345482181418,
0.534029156379));
#193321=CARTESIAN_POINT('Ctrl Pts',(-20.7225806064217,19.9371103027527,
0.534177455193948));
#193322=CARTESIAN_POINT('Origin',(-18.734,19.211,0.));
#193323=CARTESIAN_POINT('',(-20.7225807924205,19.937109793362,1.55576067791234));
#193324=CARTESIAN_POINT('',(-20.7225806064482,19.93711030268,1.33163204998037));
#193325=CARTESIAN_POINT('',(-20.7225806064498,19.9371103026755,0.));
#193326=CARTESIAN_POINT('',(-20.8509996091576,19.212286400548,1.51094372094299));
#193327=CARTESIAN_POINT('Ctrl Pts',(-20.7225807924205,19.937109793362,1.55576067791233));
#193328=CARTESIAN_POINT('Ctrl Pts',(-20.7518560701808,19.8569342392254,
1.55013149406959));
#193329=CARTESIAN_POINT('Ctrl Pts',(-20.776275590636,19.7750071948395,1.54446141602598));
#193330=CARTESIAN_POINT('Ctrl Pts',(-20.8019773243859,19.664791125207,1.53708125042421));
#193331=CARTESIAN_POINT('Ctrl Pts',(-20.80773922883,19.6376876057867,1.53528611986878));
#193332=CARTESIAN_POINT('Ctrl Pts',(-20.8211288695143,19.5680050856512,
1.53073311432502));
#193333=CARTESIAN_POINT('Ctrl Pts',(-20.8279872948907,19.5252886365728,
1.52800095498755));
#193334=CARTESIAN_POINT('Ctrl Pts',(-20.8344943181864,19.4749486713284,
1.52487275427425));
#193335=CARTESIAN_POINT('Ctrl Pts',(-20.8354165131656,19.4675032628571,
1.52441242682007));
#193336=CARTESIAN_POINT('Ctrl Pts',(-20.8368427997025,19.4554637325832,
1.52367201175446));
#193337=CARTESIAN_POINT('Ctrl Pts',(-20.8373714515695,19.4508726630248,
1.52339059474849));
#193338=CARTESIAN_POINT('Ctrl Pts',(-20.8382824843403,19.4427261589683,
1.52289293101392));
#193339=CARTESIAN_POINT('Ctrl Pts',(-20.8386708947665,19.4391714532004,
1.52267634874263));
#193340=CARTESIAN_POINT('Ctrl Pts',(-20.8394063456645,19.4322789646659,
1.52225751842798));
#193341=CARTESIAN_POINT('Ctrl Pts',(-20.8397544548719,19.4289413607279,
1.52205520894178));
#193342=CARTESIAN_POINT('Ctrl Pts',(-20.840503712184,19.4215882136833,1.52161057875839));
#193343=CARTESIAN_POINT('Ctrl Pts',(-20.8409013184691,19.4175723118643,
1.52136845553285));
#193344=CARTESIAN_POINT('Ctrl Pts',(-20.8418560173667,19.407640084005,1.52077133229358));
#193345=CARTESIAN_POINT('Ctrl Pts',(-20.842399690987,19.4017224619594,1.52041705831759));
#193346=CARTESIAN_POINT('Ctrl Pts',(-20.844583902401,19.3767968117948,1.51893080522986));
#193347=CARTESIAN_POINT('Ctrl Pts',(-20.8459924230598,19.3577687024684,
1.51781085531585));
#193348=CARTESIAN_POINT('Ctrl Pts',(-20.8496863092788,19.2966545343023,
1.51425338537026));
#193349=CARTESIAN_POINT('Ctrl Pts',(-20.8509723412249,19.2545169002474,
1.51186058233845));
#193350=CARTESIAN_POINT('Ctrl Pts',(-20.8509995586414,19.2123670084621,
1.50950273727475));
#193351=CARTESIAN_POINT('Ctrl Pts',(-20.7225806064499,19.9371103026755,
0.755484067882561));
#193352=CARTESIAN_POINT('Ctrl Pts',(-20.7109390597927,19.9689927230547,
0.757536139988532));
#193353=CARTESIAN_POINT('Ctrl Pts',(-20.6985367444623,20.0005784216913,
0.759588212094503));
#193354=CARTESIAN_POINT('Ctrl Pts',(-20.685389730172,20.0318331870602,0.761640284200474));
#193355=CARTESIAN_POINT('Ctrl Pts',(-20.6572744289615,20.0986724802413,
0.766028704574177));
#193356=CARTESIAN_POINT('Ctrl Pts',(-20.625666230531,20.1641959624094,0.770417124947881));
#193357=CARTESIAN_POINT('Ctrl Pts',(-20.5907099276933,20.2280138860434,
0.774805545321584));
#193358=CARTESIAN_POINT('Ctrl Pts',(-20.5558054909444,20.2917371204276,
0.779187454417423));
#193359=CARTESIAN_POINT('Ctrl Pts',(-20.5175630412173,20.3537594003653,
0.783569363513262));
#193360=CARTESIAN_POINT('Ctrl Pts',(-20.4761752764379,20.4137112314137,
0.787951272609101));
#193361=CARTESIAN_POINT('Ctrl Pts',(-20.4348361312034,20.4735926351085,
0.79232803413471));
#193362=CARTESIAN_POINT('Ctrl Pts',(-20.3903592835476,20.5314080265974,
0.796704795660318));
#193363=CARTESIAN_POINT('Ctrl Pts',(-20.3429822982407,20.5868142912284,
0.801081557185927));
#193364=CARTESIAN_POINT('Ctrl Pts',(-20.2956353500081,20.6421854282108,
0.805455543838661));
#193365=CARTESIAN_POINT('Ctrl Pts',(-20.2453922250265,20.6951501032064,
0.809829530491395));
#193366=CARTESIAN_POINT('Ctrl Pts',(-20.1925317157385,20.7453970262565,
0.814203517144128));
#193367=CARTESIAN_POINT('Ctrl Pts',(-20.1396872870245,20.7956286638058,
0.818576173196446));
#193368=CARTESIAN_POINT('Ctrl Pts',(-20.0842274041465,20.8431438586879,
0.822948829248764));
#193369=CARTESIAN_POINT('Ctrl Pts',(-20.0264676012165,20.8876682736325,
0.827321485301082));
#193370=CARTESIAN_POINT('Ctrl Pts',(-19.9687063209491,20.9321938273895,
0.831694253193947));
#193371=CARTESIAN_POINT('Ctrl Pts',(-19.908645387059,20.973728156449,0.836067021086812));
#193372=CARTESIAN_POINT('Ctrl Pts',(-19.8466319415337,21.0120383568039,
0.840439788979677));
#193373=CARTESIAN_POINT('Ctrl Pts',(-19.7845541598035,21.050388302296,0.844817093425684));
#193374=CARTESIAN_POINT('Ctrl Pts',(-19.7205202333155,21.0855071867432,
0.84919439787169));
#193375=CARTESIAN_POINT('Ctrl Pts',(-19.6549039955861,21.1172069223759,
0.853571702317697));
#193376=CARTESIAN_POINT('Ctrl Pts',(-19.5892519313151,21.1489239661007,
0.857951396776985));
#193377=CARTESIAN_POINT('Ctrl Pts',(-19.5220162805637,21.1772179568835,
0.862331091236272));
#193378=CARTESIAN_POINT('Ctrl Pts',(-19.4535905444954,21.2019491325176,
0.86671078569556));
#193379=CARTESIAN_POINT('Ctrl Pts',(-19.3850435794912,21.2267241240356,
0.871098239599312));
#193380=CARTESIAN_POINT('Ctrl Pts',(-19.3153027805434,21.2479235548028,
0.875485693503064));
#193381=CARTESIAN_POINT('Ctrl Pts',(-19.2447759063311,21.2654578295773,
0.879873147406816));
#193382=CARTESIAN_POINT('Ctrl Pts',(-19.1968576175474,21.2773711952502,
0.88285412856518));
#193383=CARTESIAN_POINT('Ctrl Pts',(-19.148576702708,21.2875936826828,0.885835109723544));
#193384=CARTESIAN_POINT('Ctrl Pts',(-19.1000625457264,21.2961108394079,
0.888816090881908));
#193385=CARTESIAN_POINT('Ctrl Pts',(-19.0286448051689,21.3086489546123,
0.893204396321412));
#193386=CARTESIAN_POINT('Ctrl Pts',(-18.9564428204743,21.3175380610284,
0.897592701760916));
#193387=CARTESIAN_POINT('Ctrl Pts',(-18.8838626621671,21.3226889407506,
0.90198100720042));
#193388=CARTESIAN_POINT('Ctrl Pts',(-18.8113901824199,21.3278321787243,
0.906362802232374));
#193389=CARTESIAN_POINT('Ctrl Pts',(-18.7385411199947,21.3292481656531,
0.910744597264328));
#193390=CARTESIAN_POINT('Ctrl Pts',(-18.6657304467397,21.3268989267207,
0.915126392296281));
#193391=CARTESIAN_POINT('Ctrl Pts',(-18.5930052775877,21.3245524465811,
0.919503041634105));
#193392=CARTESIAN_POINT('Ctrl Pts',(-18.5203188877622,21.3184495396718,
0.923879690971928));
#193393=CARTESIAN_POINT('Ctrl Pts',(-18.4480883541564,21.3086042359728,
0.928256340309752));
#193394=CARTESIAN_POINT('Ctrl Pts',(-18.3759035959188,21.2987651716352,
0.932630215990441));
#193395=CARTESIAN_POINT('Ctrl Pts',(-18.3041745974556,21.2851884812727,
0.937004091671129));
#193396=CARTESIAN_POINT('Ctrl Pts',(-18.2333139919643,21.2679400869635,
0.941377967351818));
#193397=CARTESIAN_POINT('Ctrl Pts',(-18.1624749209504,21.2506969344265,
0.945750513815436));
#193398=CARTESIAN_POINT('Ctrl Pts',(-18.0925041873641,21.2297844072208,
0.950123060279053));
#193399=CARTESIAN_POINT('Ctrl Pts',(-18.0238032403067,21.2053193231078,
0.954495606742671));
#193400=CARTESIAN_POINT('Ctrl Pts',(-17.9551005116343,21.1808536045441,
0.958868266599101));
#193401=CARTESIAN_POINT('Ctrl Pts',(-17.8876680885983,21.1528353098613,
0.963240926455532));
#193402=CARTESIAN_POINT('Ctrl Pts',(-17.8218896895733,21.121430260861,0.967613586311963));
#193403=CARTESIAN_POINT('Ctrl Pts',(-17.7560429990831,21.0899926069806,
0.971990785885884));
#193404=CARTESIAN_POINT('Ctrl Pts',(-17.6918541973568,21.0551613868326,
0.976367985459805));
#193405=CARTESIAN_POINT('Ctrl Pts',(-17.6296837664011,21.0171491234696,
0.980745185033726));
#193406=CARTESIAN_POINT('Ctrl Pts',(-17.5674793666564,20.9791160908995,
0.985124776229623));
#193407=CARTESIAN_POINT('Ctrl Pts',(-17.5072959315927,20.9378988273871,
0.98950436742552));
#193408=CARTESIAN_POINT('Ctrl Pts',(-17.4494639535034,20.8937525502138,
0.993883958621417));
#193409=CARTESIAN_POINT('Ctrl Pts',(-17.3915294631427,20.8495280198785,
0.998271313028188));
#193410=CARTESIAN_POINT('Ctrl Pts',(-17.3359551215016,20.8023644201836,
1.00265866743496));
#193411=CARTESIAN_POINT('Ctrl Pts',(-17.283036954651,20.7525561102443,1.00704602184173));
#193412=CARTESIAN_POINT('Ctrl Pts',(-17.2470699990045,20.7187028348753,
1.0100279804156));
#193413=CARTESIAN_POINT('Ctrl Pts',(-17.2123293106136,20.6836286139468,
1.01300993898947));
#193414=CARTESIAN_POINT('Ctrl Pts',(-17.1788971524539,20.6474345211509,
1.01599189756334));
#193415=CARTESIAN_POINT('Ctrl Pts',(-17.1297000977299,20.5941731446206,
1.0203799953476));
#193416=CARTESIAN_POINT('Ctrl Pts',(-17.0831463850142,20.5382773695794,
1.02476809313186));
#193417=CARTESIAN_POINT('Ctrl Pts',(-17.039530835554,20.4800402872808,1.02915619091612));
#193418=CARTESIAN_POINT('Ctrl Pts',(-16.9959800381062,20.4218896642455,
1.03353777409341));
#193419=CARTESIAN_POINT('Ctrl Pts',(-16.9553590315084,20.3614050170529,
1.0379193572707));
#193420=CARTESIAN_POINT('Ctrl Pts',(-16.9179243722069,20.298914663076,1.04230094044799));
#193421=CARTESIAN_POINT('Ctrl Pts',(-16.8805337207632,20.2364977722124,
1.04667737267444));
#193422=CARTESIAN_POINT('Ctrl Pts',(-16.8463222221597,20.1720802703032,
1.05105380490089));
#193423=CARTESIAN_POINT('Ctrl Pts',(-16.8155038475772,20.1060203981691,
1.05543023712734));
#193424=CARTESIAN_POINT('Ctrl Pts',(-16.7847050267982,20.0400024400483,
1.05980389257218));
#193425=CARTESIAN_POINT('Ctrl Pts',(-16.7572952618898,19.9723446153759,
1.06417754801702));
#193426=CARTESIAN_POINT('Ctrl Pts',(-16.7334424881414,19.90342952114,1.06855120346186));
#193427=CARTESIAN_POINT('Ctrl Pts',(-16.7095969789008,19.8345354154166,
1.07292352688325));
#193428=CARTESIAN_POINT('Ctrl Pts',(-16.6893064678243,19.7643852559182,
1.07729585030464));
#193429=CARTESIAN_POINT('Ctrl Pts',(-16.6726900427937,19.6933797884677,
1.08166817372603));
#193430=CARTESIAN_POINT('Ctrl Pts',(-16.6560731962969,19.6223725200037,
1.08604060804893));
#193431=CARTESIAN_POINT('Ctrl Pts',(-16.6431307288416,19.5505103706869,
1.09041304237183));
#193432=CARTESIAN_POINT('Ctrl Pts',(-16.6339309271711,19.4782057060532,
1.09478547669473));
#193433=CARTESIAN_POINT('Ctrl Pts',(-16.6247215785514,19.4058260083939,
1.09916244844239));
#193434=CARTESIAN_POINT('Ctrl Pts',(-16.6192627111906,19.3330033581393,
1.10353942019006));
#193435=CARTESIAN_POINT('Ctrl Pts',(-16.6175707663535,19.2601558640094,
1.10791639193772));
#193436=CARTESIAN_POINT('Ctrl Pts',(-16.6158778976532,19.1872685925062,
1.11229575367068));
#193437=CARTESIAN_POINT('Ctrl Pts',(-16.6179560329377,19.1143569326632,
1.11667511540364));
#193438=CARTESIAN_POINT('Ctrl Pts',(-16.623769481391,19.0418368883857,1.1210544771366));
#193439=CARTESIAN_POINT('Ctrl Pts',(-16.6295932350961,18.9691882909213,
1.12544160197716));
#193440=CARTESIAN_POINT('Ctrl Pts',(-16.6391654612832,18.8969331739607,
1.12982872681773));
#193441=CARTESIAN_POINT('Ctrl Pts',(-16.6523989007771,18.8254797492814,
1.13421585165829));
#193442=CARTESIAN_POINT('Ctrl Pts',(-16.6613997691414,18.7768799223047,
1.13719980252045));
#193443=CARTESIAN_POINT('Ctrl Pts',(-16.6720933107671,18.7286507595593,
1.14018375338261));
#193444=CARTESIAN_POINT('Ctrl Pts',(-16.6844389800457,18.6809163976466,
1.14316770424478));
#193445=CARTESIAN_POINT('Ctrl Pts',(-16.7025947167718,18.610717489178,1.14755594963142));
#193446=CARTESIAN_POINT('Ctrl Pts',(-16.7243966036732,18.5413154212983,
1.15194419501807));
#193447=CARTESIAN_POINT('Ctrl Pts',(-16.7497577469366,18.4731167564189,
1.15633244040472));
#193448=CARTESIAN_POINT('Ctrl Pts',(-16.7750812523751,18.4050193034357,
1.1607141733085));
#193449=CARTESIAN_POINT('Ctrl Pts',(-16.803953361538,18.3381221564993,1.16509590621228));
#193450=CARTESIAN_POINT('Ctrl Pts',(-16.8362368499008,18.2728187669083,
1.16947763911606));
#193451=CARTESIAN_POINT('Ctrl Pts',(-16.8684824054041,18.207592108316,1.17385422351616));
#193452=CARTESIAN_POINT('Ctrl Pts',(-16.9041311647913,18.1439559172984,
1.17823080791626));
#193453=CARTESIAN_POINT('Ctrl Pts',(-16.942997693185,18.0822840317496,1.18260739231636));
#193454=CARTESIAN_POINT('Ctrl Pts',(-16.9818395748752,18.020651254625,1.18698120136238));
#193455=CARTESIAN_POINT('Ctrl Pts',(-17.0238949203893,17.9609807185433,
1.1913550104084));
#193456=CARTESIAN_POINT('Ctrl Pts',(-17.0689328981712,17.9036207335254,
1.19572881945443));
#193457=CARTESIAN_POINT('Ctrl Pts',(-17.1139571722399,17.8462782014402,
1.20010129768081));
#193458=CARTESIAN_POINT('Ctrl Pts',(-17.1619619791427,17.7912452038486,
1.2044737759072));
#193459=CARTESIAN_POINT('Ctrl Pts',(-17.2126747882375,17.7388387995685,
1.20884625413359));
#193460=CARTESIAN_POINT('Ctrl Pts',(-17.2633888949715,17.6864310543136,
1.21321884424293));
#193461=CARTESIAN_POINT('Ctrl Pts',(-17.3168108045951,17.6366503810584,
1.21759143435227));
#193462=CARTESIAN_POINT('Ctrl Pts',(-17.3726307197092,17.5897774111244,
1.22196402446161));
#193463=CARTESIAN_POINT('Ctrl Pts',(-17.4285085645615,17.5428557965647,
1.22634115243167));
#193464=CARTESIAN_POINT('Ctrl Pts',(-17.4867890134539,17.4988482210374,
1.23071828040173));
#193465=CARTESIAN_POINT('Ctrl Pts',(-17.547129377997,17.4579948298347,1.23509540837179));
#193466=CARTESIAN_POINT('Ctrl Pts',(-17.6075026960962,17.4171191274556,
1.23947492681353));
#193467=CARTESIAN_POINT('Ctrl Pts',(-17.669937756504,17.3794012886564,1.24385444525527));
#193468=CARTESIAN_POINT('Ctrl Pts',(-17.7340654232695,17.3450364842101,
1.248233963697));
#193469=CARTESIAN_POINT('Ctrl Pts',(-17.7983067483476,17.3106107724227,
1.25262124429041));
#193470=CARTESIAN_POINT('Ctrl Pts',(-17.8642462337679,17.2795501683287,
1.25700852488382));
#193471=CARTESIAN_POINT('Ctrl Pts',(-17.9314933831593,17.2520022639301,
1.26139580547722));
#193472=CARTESIAN_POINT('Ctrl Pts',(-17.9772094535304,17.2332746011599,
1.26437837396022));
#193473=CARTESIAN_POINT('Ctrl Pts',(-18.0235294697532,17.2161693410616,
1.26736094244321));
#193474=CARTESIAN_POINT('Ctrl Pts',(-18.0703272881676,17.2007195390769,
1.27034351092621));
#193475=CARTESIAN_POINT('Ctrl Pts',(-18.1391803751295,17.1779884247721,
1.2747317293109));
#193476=CARTESIAN_POINT('Ctrl Pts',(-18.2093370328472,17.1587544122963,
1.27911994769558));
#193477=CARTESIAN_POINT('Ctrl Pts',(-18.2804083779596,17.1431645035413,
1.28350816608027));
#193478=CARTESIAN_POINT('Ctrl Pts',(-18.3513742462393,17.1275977317368,
1.28788987191936));
#193479=CARTESIAN_POINT('Ctrl Pts',(-18.4232516398406,17.1156644301232,
1.29227157775844));
#193480=CARTESIAN_POINT('Ctrl Pts',(-18.4956354563143,17.1074621837691,
1.29665328359752));
#193481=CARTESIAN_POINT('Ctrl Pts',(-18.5679342224827,17.0992695749775,
1.30102984097336));
#193482=CARTESIAN_POINT('Ctrl Pts',(-18.6407377525394,17.0947993667338,
1.3054063983492));
#193483=CARTESIAN_POINT('Ctrl Pts',(-18.7136313401116,17.0940979905309,
1.30978295572503));
#193484=CARTESIAN_POINT('Ctrl Pts',(-18.7864787035313,17.0933970590931,
1.31415673778602));
#193485=CARTESIAN_POINT('Ctrl Pts',(-18.8594155299897,17.0964602223804,
1.31853051984701));
#193486=CARTESIAN_POINT('Ctrl Pts',(-18.9320240054094,17.1032819227227,
1.322904301908));
#193487=CARTESIAN_POINT('Ctrl Pts',(-19.0046103894158,17.1101015475359,
1.32727675322865));
#193488=CARTESIAN_POINT('Ctrl Pts',(-19.0768681407482,17.120677394011,1.3316492045493));
#193489=CARTESIAN_POINT('Ctrl Pts',(-19.148383151568,17.1349519264486,1.33602165586994));
#193490=CARTESIAN_POINT('Ctrl Pts',(-19.219899994278,17.149226824535,1.34039421919296));
#193491=CARTESIAN_POINT('Ctrl Pts',(-19.2906735860492,17.1672005003068,
1.34476678251598));
#193492=CARTESIAN_POINT('Ctrl Pts',(-19.3603002769535,17.1887643650929,
1.349139345839));
#193493=CARTESIAN_POINT('Ctrl Pts',(-19.4299992325989,17.2103506107661,
1.35351644739516));
#193494=CARTESIAN_POINT('Ctrl Pts',(-19.4985484489852,17.235534342081,1.35789354895132));
#193495=CARTESIAN_POINT('Ctrl Pts',(-19.5655605152348,17.2641573999158,
1.36227065050748));
#193496=CARTESIAN_POINT('Ctrl Pts',(-19.632609181428,17.2927960907905,1.3666501427028));
#193497=CARTESIAN_POINT('Ctrl Pts',(-19.6981185924442,17.3248776358673,
1.37102963489813));
#193498=CARTESIAN_POINT('Ctrl Pts',(-19.7617248384167,17.3601972940096,
1.37540912709345));
#193499=CARTESIAN_POINT('Ctrl Pts',(-19.8254438274278,17.3955795567832,
1.37979638200532));
#193500=CARTESIAN_POINT('Ctrl Pts',(-19.8872525054644,17.4342111384903,
1.38418363691718));
#193501=CARTESIAN_POINT('Ctrl Pts',(-19.9468154069978,17.4758435838379,
1.38857089182904));
#193502=CARTESIAN_POINT('Ctrl Pts',(-19.9873110558898,17.5041486671347,
1.39155370042191));
#193503=CARTESIAN_POINT('Ctrl Pts',(-20.0267692619178,17.5338399735792,
1.39453650901478));
#193504=CARTESIAN_POINT('Ctrl Pts',(-20.0650939283882,17.5648293059928,
1.39751931760765));
#193505=CARTESIAN_POINT('Ctrl Pts',(-20.1207402998965,17.6098249723118,
1.4018502744139));
#193506=CARTESIAN_POINT('Ctrl Pts',(-20.1742249041617,17.6577445690432,
1.40618123122015));
#193507=CARTESIAN_POINT('Ctrl Pts',(-20.2252181563952,17.7083498710487,
1.4105121880264));
#193508=CARTESIAN_POINT('Ctrl Pts',(-20.2761246600306,17.7588690844285,
1.41483577710427));
#193509=CARTESIAN_POINT('Ctrl Pts',(-20.3245478783115,17.8120645847693,
1.41915936618215));
#193510=CARTESIAN_POINT('Ctrl Pts',(-20.3701907287601,17.8676575644611,
1.42348295526002));
#193511=CARTESIAN_POINT('Ctrl Pts',(-20.415790130129,17.9231976231856,1.42780242855714));
#193512=CARTESIAN_POINT('Ctrl Pts',(-20.4586140966688,17.9811302563624,
1.43212190185425));
#193513=CARTESIAN_POINT('Ctrl Pts',(-20.4984028945192,18.0411404247464,
1.43644137515136));
#193514=CARTESIAN_POINT('Ctrl Pts',(-20.5381677566161,18.101114492804,1.44075824998224));
#193515=CARTESIAN_POINT('Ctrl Pts',(-20.5749007972635,18.1631632051077,
1.44507512481312));
#193516=CARTESIAN_POINT('Ctrl Pts',(-20.6083841924735,18.2269406018916,
1.44939199964401));
#193517=CARTESIAN_POINT('Ctrl Pts',(-20.6418591738518,18.2907019724546,
1.45370778971456));
#193518=CARTESIAN_POINT('Ctrl Pts',(-20.672085900762,18.3561907258456,1.45802357978511));
#193519=CARTESIAN_POINT('Ctrl Pts',(-20.6988922453411,18.423035873787,1.46233936985566));
#193520=CARTESIAN_POINT('Ctrl Pts',(-20.7257171930929,18.489927411188,1.46665815501524));
#193521=CARTESIAN_POINT('Ctrl Pts',(-20.7491168291636,18.5581767631563,
1.47097694017482));
#193522=CARTESIAN_POINT('Ctrl Pts',(-20.7689674532606,18.6273935708287,
1.47529572533439));
#193523=CARTESIAN_POINT('Ctrl Pts',(-20.7888248459354,18.6966339797413,
1.47961598309418));
#193524=CARTESIAN_POINT('Ctrl Pts',(-20.8051307022979,18.7668420178477,
1.48393624085397));
#193525=CARTESIAN_POINT('Ctrl Pts',(-20.8178121286519,18.8376154629832,
1.48825649861375));
#193526=CARTESIAN_POINT('Ctrl Pts',(-20.8305133213042,18.908499221343,1.49258349027723));
#193527=CARTESIAN_POINT('Ctrl Pts',(-20.8395787385446,18.9799496538715,
1.49691048194071));
#193528=CARTESIAN_POINT('Ctrl Pts',(-20.8449873102489,19.0515585500307,
1.50123747360419));
#193529=CARTESIAN_POINT('Ctrl Pts',(-20.8490314544484,19.1051025756753,
1.50447288938379));
#193530=CARTESIAN_POINT('Ctrl Pts',(-20.8510321497683,19.1587350706587,
1.50770830516339));
#193531=CARTESIAN_POINT('Ctrl Pts',(-20.8509996091576,19.212286400548,1.51094372094299));
#193532=CARTESIAN_POINT('Ctrl Pts',(-20.7225806064217,19.9371103027527,
0.534177455193948));
#193533=CARTESIAN_POINT('Ctrl Pts',(-20.7114374698477,19.9676277395686,
0.535943868253035));
#193534=CARTESIAN_POINT('Ctrl Pts',(-20.6995931583947,19.9978850480326,
0.537705158541846));
#193535=CARTESIAN_POINT('Ctrl Pts',(-20.6589746514824,20.0950013681374,
0.543420670497742));
#193536=CARTESIAN_POINT('Ctrl Pts',(-20.6274494476113,20.1606495982188,
0.547383443423855));
#193537=CARTESIAN_POINT('Ctrl Pts',(-20.5661685037545,20.2730250582085,
0.554496407985185));
#193538=CARTESIAN_POINT('Ctrl Pts',(-20.5378441393874,20.3204522608092,
0.557608779156871));
#193539=CARTESIAN_POINT('Ctrl Pts',(-20.4889707980559,20.3954591389319,
0.562757557262939));
#193540=CARTESIAN_POINT('Ctrl Pts',(-20.4695469282906,20.4237417762343,
0.564754091976727));
#193541=CARTESIAN_POINT('Ctrl Pts',(-20.4431388558086,20.4602594569332,
0.567411436815425));
#193542=CARTESIAN_POINT('Ctrl Pts',(-20.4367661664181,20.4689317132342,
0.56804855313285));
#193543=CARTESIAN_POINT('Ctrl Pts',(-20.426225873687,20.4830485833113,0.569095795672003));
#193544=CARTESIAN_POINT('Ctrl Pts',(-20.422097403048,20.4885222745581,0.569504380689825));
#193545=CARTESIAN_POINT('Ctrl Pts',(-20.4140585932407,20.4990734427671,
0.570296928178457));
#193546=CARTESIAN_POINT('Ctrl Pts',(-20.4101516393926,20.504153413573,0.570680753597797));
#193547=CARTESIAN_POINT('Ctrl Pts',(-20.401083709184,20.5158337467052,0.5715685206328));
#193548=CARTESIAN_POINT('Ctrl Pts',(-20.3959065203337,20.5224213336935,
0.572073108100753));
#193549=CARTESIAN_POINT('Ctrl Pts',(-20.3818932677003,20.540035908778,0.573432938593689));
#193550=CARTESIAN_POINT('Ctrl Pts',(-20.3729857963623,20.5510053031887,
0.574291057870885));
#193551=CARTESIAN_POINT('Ctrl Pts',(-20.2682894327803,20.6773313240747,
0.58430710600086));
#193552=CARTESIAN_POINT('Ctrl Pts',(-20.1606341987796,20.7822639584046,
0.593981499501864));
#193553=CARTESIAN_POINT('Ctrl Pts',(-19.9681110289533,20.9336998234509,
0.610137699571716));
#193554=CARTESIAN_POINT('Ctrl Pts',(-19.8895240311662,20.9873697509775,
0.616462819861445));
#193555=CARTESIAN_POINT('Ctrl Pts',(-19.7687998424279,21.0584047934686,
0.625584594307354));
#193556=CARTESIAN_POINT('Ctrl Pts',(-19.729283565231,21.0799907259246,0.628482435959696));
#193557=CARTESIAN_POINT('Ctrl Pts',(-19.6670847064776,21.111434381759,0.632877663235488));
#193558=CARTESIAN_POINT('Ctrl Pts',(-19.6448686052041,21.122181942398,0.634415809433181));
#193559=CARTESIAN_POINT('Ctrl Pts',(-19.6165125588766,21.1352930237958,
0.636334506882315));
#193560=CARTESIAN_POINT('Ctrl Pts',(-19.6105436868814,21.1380192592776,
0.636735918909718));
#193561=CARTESIAN_POINT('Ctrl Pts',(-19.6015000360848,21.1420991616775,
0.637340279196587));
#193562=CARTESIAN_POINT('Ctrl Pts',(-19.5984346187612,21.1434733051433,
0.637544468859004));
#193563=CARTESIAN_POINT('Ctrl Pts',(-19.5921230212518,21.1462846000517,
0.637963506613385));
#193564=CARTESIAN_POINT('Ctrl Pts',(-19.5888765445637,21.1477208617937,
0.638178292203626));
#193565=CARTESIAN_POINT('Ctrl Pts',(-19.581585601535,21.1509245162282,0.63865899169706));
#193566=CARTESIAN_POINT('Ctrl Pts',(-19.5775392164236,21.1526874289545,
0.638924629429125));
#193567=CARTESIAN_POINT('Ctrl Pts',(-19.5672279888454,21.1571414666062,
0.639598706191506));
#193568=CARTESIAN_POINT('Ctrl Pts',(-19.5609555503574,21.1598150271458,
0.640006098720852));
#193569=CARTESIAN_POINT('Ctrl Pts',(-19.5252605404774,21.174826278749,0.642310020582687));
#193570=CARTESIAN_POINT('Ctrl Pts',(-19.495573241086,21.1865286231352,0.644170573075016));
#193571=CARTESIAN_POINT('Ctrl Pts',(-19.2794566774673,21.2661224387947,
0.657394742669097));
#193572=CARTESIAN_POINT('Ctrl Pts',(-19.0845510714179,21.3081849084335,
0.667705270028045));
#193573=CARTESIAN_POINT('Ctrl Pts',(-18.8308754209566,21.3265206893776,
0.681839342496874));
#193574=CARTESIAN_POINT('Ctrl Pts',(-18.7749971092634,21.3283405967854,
0.684989197358653));
#193575=CARTESIAN_POINT('Ctrl Pts',(-18.6844318490127,21.3277038002695,
0.690198340708285));
#193576=CARTESIAN_POINT('Ctrl Pts',(-18.649761525261,21.3266076329026,0.692217031247737));
#193577=CARTESIAN_POINT('Ctrl Pts',(-18.6042836795442,21.3240501184867,
0.694903282787265));
#193578=CARTESIAN_POINT('Ctrl Pts',(-18.5934372163466,21.3233563203746,
0.695546808780345));
#193579=CARTESIAN_POINT('Ctrl Pts',(-18.5756919081778,21.3220839560979,
0.696604502968437));
#193580=CARTESIAN_POINT('Ctrl Pts',(-18.5687896233513,21.3215550102596,
0.697017111806223));
#193581=CARTESIAN_POINT('Ctrl Pts',(-18.5554413934161,21.3204662089668,
0.697817428969723));
#193582=CARTESIAN_POINT('Ctrl Pts',(-18.5489951691573,21.3199106367706,
0.698204998525948));
#193583=CARTESIAN_POINT('Ctrl Pts',(-18.5341276419443,21.3185605778978,
0.699101409454807));
#193584=CARTESIAN_POINT('Ctrl Pts',(-18.5257083933891,21.3177451560176,
0.699610903010173));
#193585=CARTESIAN_POINT('Ctrl Pts',(-18.5031019851936,21.3154188421011,
0.700984062019599));
#193586=CARTESIAN_POINT('Ctrl Pts',(-18.4889250260433,21.3138149699328,
0.701850632083286));
#193587=CARTESIAN_POINT('Ctrl Pts',(-18.3611862263606,21.2980542766511,
0.709709002707594));
#193588=CARTESIAN_POINT('Ctrl Pts',(-18.248948460074,21.2748564259868,0.716988808719096));
#193589=CARTESIAN_POINT('Ctrl Pts',(-17.9820744672696,21.1967201284121,
0.735129537826583));
#193590=CARTESIAN_POINT('Ctrl Pts',(-17.8308675718973,21.132673214878,0.746147032977224));
#193591=CARTESIAN_POINT('Ctrl Pts',(-17.6600530146194,21.0356645800402,
0.758629156568118));
#193592=CARTESIAN_POINT('Ctrl Pts',(-17.6319343410552,21.0188203764615,
0.76068315406141));
#193593=CARTESIAN_POINT('Ctrl Pts',(-17.5980616863358,20.9974451050083,
0.76314606236294));
#193594=CARTESIAN_POINT('Ctrl Pts',(-17.5919269198305,20.9935293963174,
0.76359165733612));
#193595=CARTESIAN_POINT('Ctrl Pts',(-17.5823436971568,20.9873428177069,
0.76428683906326));
#193596=CARTESIAN_POINT('Ctrl Pts',(-17.5788815510295,20.9850934066207,
0.764537805163716));
#193597=CARTESIAN_POINT('Ctrl Pts',(-17.5724290481779,20.9808742174639,
0.765005161661114));
#193598=CARTESIAN_POINT('Ctrl Pts',(-17.5694371343737,20.9789069981398,
0.765221711043567));
#193599=CARTESIAN_POINT('Ctrl Pts',(-17.5626239308124,20.9744024339311,
0.765714494814857));
#193600=CARTESIAN_POINT('Ctrl Pts',(-17.5588058968779,20.97186026145,0.765990401383822));
#193601=CARTESIAN_POINT('Ctrl Pts',(-17.547098640409,20.964010146944,0.766835764363602));
#193602=CARTESIAN_POINT('Ctrl Pts',(-17.5392367670136,20.9586613623376,
0.767402546263394));
#193603=CARTESIAN_POINT('Ctrl Pts',(-17.4690404166341,20.9102085642016,
0.772457519535672));
#193604=CARTESIAN_POINT('Ctrl Pts',(-17.4090192225959,20.8638342390826,
0.776740255607443));
#193605=CARTESIAN_POINT('Ctrl Pts',(-17.2444280988522,20.7219242508775,
0.788770466806824));
#193606=CARTESIAN_POINT('Ctrl Pts',(-17.1467824827809,20.618998372626,0.796293125138248));
#193607=CARTESIAN_POINT('Ctrl Pts',(-17.022285476647,20.4582146529618,0.807543735498695));
#193608=CARTESIAN_POINT('Ctrl Pts',(-16.9865976887691,20.4077018443386,
0.811013100431889));
#193609=CARTESIAN_POINT('Ctrl Pts',(-16.9330234067257,20.3243557103918,
0.81669936314064));
#193610=CARTESIAN_POINT('Ctrl Pts',(-16.9137060555985,20.2924838573702,
0.818865114738588));
#193611=CARTESIAN_POINT('Ctrl Pts',(-16.8897205357709,20.250445205352,0.821718259343063));
#193612=CARTESIAN_POINT('Ctrl Pts',(-16.8842769220177,20.2407269563917,
0.822377583893358));
#193613=CARTESIAN_POINT('Ctrl Pts',(-16.8755506591457,20.2248558443021,
0.823454136645717));
#193614=CARTESIAN_POINT('Ctrl Pts',(-16.87222122739,20.2187288452848,0.823869686985817));
#193615=CARTESIAN_POINT('Ctrl Pts',(-16.8658779938211,20.2069169494291,
0.824670757746429));
#193616=CARTESIAN_POINT('Ctrl Pts',(-16.8628597153497,20.2012345347806,
0.825056113291186));
#193617=CARTESIAN_POINT('Ctrl Pts',(-16.8560099819751,20.1881956251176,
0.825940349676464));
#193618=CARTESIAN_POINT('Ctrl Pts',(-16.8521957806587,20.1808302297633,
0.826439833340899));
#193619=CARTESIAN_POINT('Ctrl Pts',(-16.842181493918,20.1612106837186,0.827770418671016));
#193620=CARTESIAN_POINT('Ctrl Pts',(-16.8360572773322,20.1489184457796,
0.828604162700456));
#193621=CARTESIAN_POINT('Ctrl Pts',(-16.7905179108019,20.0552413115783,
0.834959650078114));
#193622=CARTESIAN_POINT('Ctrl Pts',(-16.7562390824143,19.9714761892541,
0.840658245854226));
#193623=CARTESIAN_POINT('Ctrl Pts',(-16.6828174720997,19.7531458591501,
0.855531878553615));
#193624=CARTESIAN_POINT('Ctrl Pts',(-16.6514759899623,19.6164142017218,
0.864883255525189));
#193625=CARTESIAN_POINT('Ctrl Pts',(-16.6269184297165,19.4229668070138,
0.877654126274579));
#193626=CARTESIAN_POINT('Ctrl Pts',(-16.6221165608976,19.368072730332,0.881223466303394));
#193627=CARTESIAN_POINT('Ctrl Pts',(-16.618091488661,19.2846711192318,0.8865082084408));
#193628=CARTESIAN_POINT('Ctrl Pts',(-16.6172932451848,19.256265439619,0.888283820194297));
#193629=CARTESIAN_POINT('Ctrl Pts',(-16.6170118446478,19.2209135315712,
0.890456405932284));
#193630=CARTESIAN_POINT('Ctrl Pts',(-16.616990724002,19.2139759749343,0.890880975800615));
#193631=CARTESIAN_POINT('Ctrl Pts',(-16.6170112720142,19.2029957409646,
0.891549994766704));
#193632=CARTESIAN_POINT('Ctrl Pts',(-16.6170304167401,19.1989531428592,
0.891795673262578));
#193633=CARTESIAN_POINT('Ctrl Pts',(-16.6170883596838,19.1913293931787,
0.892257758602559));
#193634=CARTESIAN_POINT('Ctrl Pts',(-16.617124664591,19.1877483289616,0.892474296362578));
#193635=CARTESIAN_POINT('Ctrl Pts',(-16.617228450216,19.179560689524,0.892968224096466));
#193636=CARTESIAN_POINT('Ctrl Pts',(-16.6173018807224,19.1749542376282,
0.89324527811114));
#193637=CARTESIAN_POINT('Ctrl Pts',(-16.6175368056402,19.1627225024376,
0.893978822222175));
#193638=CARTESIAN_POINT('Ctrl Pts',(-16.6177244726278,19.1550977096705,
0.89443388610738));
#193639=CARTESIAN_POINT('Ctrl Pts',(-16.6193295470784,19.1016328178291,
0.897610394406912));
#193640=CARTESIAN_POINT('Ctrl Pts',(-16.6221951265029,19.0558447313641,
0.900256665027179));
#193641=CARTESIAN_POINT('Ctrl Pts',(-16.6301237549122,18.9726387903883,
0.904988039765976));
#193642=CARTESIAN_POINT('Ctrl Pts',(-16.63470400901,18.9351959136889,0.907088386485106));
#193643=CARTESIAN_POINT('Ctrl Pts',(-16.6596402980374,18.768448723022,0.916388591586645));
#193644=CARTESIAN_POINT('Ctrl Pts',(-16.690960810843,18.6410770633278,0.92336600192118));
#193645=CARTESIAN_POINT('Ctrl Pts',(-16.762785710537,18.4339500931436,0.93546669699205));
#193646=CARTESIAN_POINT('Ctrl Pts',(-16.7969195885184,18.3523910980012,
0.940438786075902));
#193647=CARTESIAN_POINT('Ctrl Pts',(-16.8451366111527,18.2548068412481,
0.946782362698708));
#193648=CARTESIAN_POINT('Ctrl Pts',(-16.8544954963979,18.2365396181598,
0.947987380284465));
#193649=CARTESIAN_POINT('Ctrl Pts',(-16.8682706809051,18.2105893133332,
0.949725728871437));
#193650=CARTESIAN_POINT('Ctrl Pts',(-16.8724720934033,18.2027930354066,
0.950251454969338));
#193651=CARTESIAN_POINT('Ctrl Pts',(-16.8798389662669,18.1893258654414,
0.951165723955367));
#193652=CARTESIAN_POINT('Ctrl Pts',(-16.8829818528705,18.1836427136646,
0.951553456515558));
#193653=CARTESIAN_POINT('Ctrl Pts',(-16.8890741111731,18.1727450437957,
0.952300670518855));
#193654=CARTESIAN_POINT('Ctrl Pts',(-16.8920195687416,18.1675284004536,
0.952660008432743));
#193655=CARTESIAN_POINT('Ctrl Pts',(-16.8997914922062,18.1538991455451,
0.953603205191064));
#193656=CARTESIAN_POINT('Ctrl Pts',(-16.9046536566807,18.1455071479193,
0.954188351430258));
#193657=CARTESIAN_POINT('Ctrl Pts',(-16.9217169765652,18.1165173009355,
0.956225180389785));
#193658=CARTESIAN_POINT('Ctrl Pts',(-16.9342093846982,18.0960938143696,
0.95768743621197));
#193659=CARTESIAN_POINT('Ctrl Pts',(-17.0303114782358,17.9448047871347,
0.968729742983238));
#193660=CARTESIAN_POINT('Ctrl Pts',(-17.127733439411,17.8233054871346,0.978845965486544));
#193661=CARTESIAN_POINT('Ctrl Pts',(-17.290118875248,17.661025224386,0.994012844950908));
#193662=CARTESIAN_POINT('Ctrl Pts',(-17.3454300549669,17.6112848483738,
0.998936010626699));
#193663=CARTESIAN_POINT('Ctrl Pts',(-17.4390016825733,17.5356545883667,
1.00677218781032));
#193664=CARTESIAN_POINT('Ctrl Pts',(-17.4756936447651,17.5079237972352,
1.0097329997917));
#193665=CARTESIAN_POINT('Ctrl Pts',(-17.5269182487629,17.4717696967445,
1.01368766850648));
#193666=CARTESIAN_POINT('Ctrl Pts',(-17.5406888215884,17.4622928003012,
1.01473383612806));
#193667=CARTESIAN_POINT('Ctrl Pts',(-17.5644672947668,17.4463401805657,
1.01650955099053));
#193668=CARTESIAN_POINT('Ctrl Pts',(-17.5744201013412,17.4397841744795,
1.01724374437526));
#193669=CARTESIAN_POINT('Ctrl Pts',(-17.5886442672696,17.4305858750477,
1.01827962017682));
#193670=CARTESIAN_POINT('Ctrl Pts',(-17.5928702713742,17.4278743301528,
1.01858571432806));
#193671=CARTESIAN_POINT('Ctrl Pts',(-17.6001689201298,17.4232278482474,
1.01911144572552));
#193672=CARTESIAN_POINT('Ctrl Pts',(-17.6032369543778,17.4212857435601,
1.01933155604431));
#193673=CARTESIAN_POINT('Ctrl Pts',(-17.6091968425474,17.4175345020901,
1.01975740601362));
#193674=CARTESIAN_POINT('Ctrl Pts',(-17.612088068981,17.4157244627561,1.01996320863873));
#193675=CARTESIAN_POINT('Ctrl Pts',(-17.6198977229054,17.4108614978265,
1.02051703990849));
#193676=CARTESIAN_POINT('Ctrl Pts',(-17.6248243603994,17.4078217189798,
1.02086420742884));
#193677=CARTESIAN_POINT('Ctrl Pts',(-17.643140021943,17.3966242621233,1.02214692548973));
#193678=CARTESIAN_POINT('Ctrl Pts',(-17.6566074506474,17.3885949580349,
1.02307443826268));
#193679=CARTESIAN_POINT('Ctrl Pts',(-17.7862402628644,17.3132470190554,
1.03186578656901));
#193680=CARTESIAN_POINT('Ctrl Pts',(-17.9084891445359,17.2569640131818,
1.03912833110805));
#193681=CARTESIAN_POINT('Ctrl Pts',(-18.1869536715711,17.1595972085844,
1.05514807789573));
#193682=CARTESIAN_POINT('Ctrl Pts',(-18.3441708786778,17.1240073815863,
1.06389542625938));
#193683=CARTESIAN_POINT('Ctrl Pts',(-18.5224424529483,17.1045146268698,
1.07436838051043));
#193684=CARTESIAN_POINT('Ctrl Pts',(-18.5410181714938,17.1027317049779,
1.07546550415108));
#193685=CARTESIAN_POINT('Ctrl Pts',(-18.5681149000296,17.1004920321706,
1.07707532954445));
#193686=CARTESIAN_POINT('Ctrl Pts',(-18.5766192676691,17.099840827766,1.07758192585691));
#193687=CARTESIAN_POINT('Ctrl Pts',(-18.5915587880994,17.0987876357999,
1.07847431431548));
#193688=CARTESIAN_POINT('Ctrl Pts',(-18.597992313621,17.0983636190404,1.07885940979307));
#193689=CARTESIAN_POINT('Ctrl Pts',(-18.6105048785615,17.0975963407544,
1.07960997350512));
#193690=CARTESIAN_POINT('Ctrl Pts',(-18.6165836651595,17.0972499024151,
1.07997533803777));
#193691=CARTESIAN_POINT('Ctrl Pts',(-18.6311454515579,17.0964830150636,
1.08085235508423));
#193692=CARTESIAN_POINT('Ctrl Pts',(-18.6396296031234,17.0960873865274,
1.08136478132736));
#193693=CARTESIAN_POINT('Ctrl Pts',(-18.6704139673352,17.0948374722322,
1.08322948010482));
#193694=CARTESIAN_POINT('Ctrl Pts',(-18.6927243427418,17.0942847882159,
1.08459114742374));
#193695=CARTESIAN_POINT('Ctrl Pts',(-18.8983629639602,17.0924428680754,
1.09724057980109));
#193696=CARTESIAN_POINT('Ctrl Pts',(-19.0810914412825,17.1146220681367,
1.10930521320479));
#193697=CARTESIAN_POINT('Ctrl Pts',(-19.3376248031391,17.1802430190148,
1.12678928365928));
#193698=CARTESIAN_POINT('Ctrl Pts',(-19.4153877710262,17.2049966894788,
1.13214940984021));
#193699=CARTESIAN_POINT('Ctrl Pts',(-19.5255261418308,17.247202513244,1.13967034698697));
#193700=CARTESIAN_POINT('Ctrl Pts',(-19.5591798243294,17.2611044058583,
1.14195798478512));
#193701=CARTESIAN_POINT('Ctrl Pts',(-19.5993087210326,17.2789063308987,
1.14465893236394));
#193702=CARTESIAN_POINT('Ctrl Pts',(-19.6061409649305,17.2819807491836,
1.14511783251375));
#193703=CARTESIAN_POINT('Ctrl Pts',(-19.6167472553775,17.2868213069696,
1.14582856644189));
#193704=CARTESIAN_POINT('Ctrl Pts',(-19.6205325734649,17.288562392049,1.14608189278049));
#193705=CARTESIAN_POINT('Ctrl Pts',(-19.6275487043413,17.2918146430756,
1.14655078837561));
#193706=CARTESIAN_POINT('Ctrl Pts',(-19.6307808095771,17.2933227849476,
1.14676653356323));
#193707=CARTESIAN_POINT('Ctrl Pts',(-19.6380869564188,17.2967544378917,
1.14725364736596));
#193708=CARTESIAN_POINT('Ctrl Pts',(-19.6421586674959,17.2986827845956,
1.14752471290317));
#193709=CARTESIAN_POINT('Ctrl Pts',(-19.6544483244028,17.3045512228829,
1.14834174357124));
#193710=CARTESIAN_POINT('Ctrl Pts',(-19.6626471361992,17.3085314560192,
1.14888528194622));
#193711=CARTESIAN_POINT('Ctrl Pts',(-19.7255937638177,17.3395937029289,
1.15304844641102));
#193712=CARTESIAN_POINT('Ctrl Pts',(-19.7791775080496,17.3689833971257,
1.15653489960124));
#193713=CARTESIAN_POINT('Ctrl Pts',(-19.9708586361236,17.4851791353637,
1.16906415693261));
#193714=CARTESIAN_POINT('Ctrl Pts',(-20.100068947161,17.5855344379555,1.1776651801176));
#193715=CARTESIAN_POINT('Ctrl Pts',(-20.2731079113415,17.7552777135112,
1.19111372097631));
#193716=CARTESIAN_POINT('Ctrl Pts',(-20.3265598745273,17.8139561135951,
1.1956010316147));
#193717=CARTESIAN_POINT('Ctrl Pts',(-20.3888156884265,17.8905267612264,
1.20135967524924));
#193718=CARTESIAN_POINT('Ctrl Pts',(-20.4008334404232,17.9057296134612,
1.20249840406351));
#193719=CARTESIAN_POINT('Ctrl Pts',(-20.4179162397091,17.9279606130509,
1.20415796085933));
#193720=CARTESIAN_POINT('Ctrl Pts',(-20.4231497435415,17.9348585065455,
1.20467212634369));
#193721=CARTESIAN_POINT('Ctrl Pts',(-20.4322172775493,17.9469632573573,
1.20557316958583));
#193722=CARTESIAN_POINT('Ctrl Pts',(-20.4360700664591,17.9521559683779,
1.20595930643275));
#193723=CARTESIAN_POINT('Ctrl Pts',(-20.4434807364971,17.9622401368593,
1.2067084576106));
#193724=CARTESIAN_POINT('Ctrl Pts',(-20.4470415660781,17.9671293572265,
1.20707135210618));
#193725=CARTESIAN_POINT('Ctrl Pts',(-20.4554657382686,17.9788010042822,
1.207936925831));
#193726=CARTESIAN_POINT('Ctrl Pts',(-20.4603099945613,17.9855970243881,
1.20844033487524));
#193727=CARTESIAN_POINT('Ctrl Pts',(-20.4774345686988,18.009924210953,1.21024038985446));
#193728=CARTESIAN_POINT('Ctrl Pts',(-20.4894887237817,18.0276123060267,
1.21154561110807));
#193729=CARTESIAN_POINT('Ctrl Pts',(-20.6070117123993,18.2058117832186,
1.22466387062213));
#193730=CARTESIAN_POINT('Ctrl Pts',(-20.6904215902378,18.3797598360829,
1.23734178450062));
#193731=CARTESIAN_POINT('Ctrl Pts',(-20.7725200131164,18.6348873195065,
1.25502398947527));
#193732=CARTESIAN_POINT('Ctrl Pts',(-20.7918958078666,18.7084703105442,
1.26000962831794));
#193733=CARTESIAN_POINT('Ctrl Pts',(-20.8143280450851,18.8171190742397,
1.26707459920589));
#193734=CARTESIAN_POINT('Ctrl Pts',(-20.820538957625,18.8514691043632,1.2692655558093));
#193735=CARTESIAN_POINT('Ctrl Pts',(-20.8270336481075,18.8932676428165,
1.27186758279374));
#193736=CARTESIAN_POINT('Ctrl Pts',(-20.8281309513188,18.9005821117358,
1.2723205554791));
#193737=CARTESIAN_POINT('Ctrl Pts',(-20.8297832003394,18.9120034307894,
1.2730240118857));
#193738=CARTESIAN_POINT('Ctrl Pts',(-20.8303644473172,18.9161063311484,
1.27327594252214));
#193739=CARTESIAN_POINT('Ctrl Pts',(-20.8314236226128,18.9237442402589,
1.27374346151841));
#193740=CARTESIAN_POINT('Ctrl Pts',(-20.8319046586926,18.9272787151129,
1.27395921812063));
#193741=CARTESIAN_POINT('Ctrl Pts',(-20.8329764096804,18.9353053158722,
1.27444786561784));
#193742=CARTESIAN_POINT('Ctrl Pts',(-20.8335616374145,18.9397981216413,
1.27472044424227));
#193743=CARTESIAN_POINT('Ctrl Pts',(-20.8352591883987,18.953165147939,1.27552872938973));
#193744=CARTESIAN_POINT('Ctrl Pts',(-20.8363297207846,18.9620447043229,
1.27606213717881));
#193745=CARTESIAN_POINT('Ctrl Pts',(-20.8440773401224,19.0299247942671,
1.28011469178529));
#193746=CARTESIAN_POINT('Ctrl Pts',(-20.8483264336687,19.0891816749318,
1.28350793907857));
#193747=CARTESIAN_POINT('Ctrl Pts',(-20.8506770365375,19.1688228885189,
1.28796720666029));
#193748=CARTESIAN_POINT('Ctrl Pts',(-20.8509840406832,19.1891096026186,
1.28909428040348));
#193749=CARTESIAN_POINT('Ctrl Pts',(-20.8511051845503,19.3491947094905,
1.29793919539568));
#193750=CARTESIAN_POINT('Ctrl Pts',(-20.8373639130496,19.4886586124641,
1.3053742556948));
#193751=CARTESIAN_POINT('Ctrl Pts',(-20.7922498000778,19.714469502803,1.31812049820498));
#193752=CARTESIAN_POINT('Ctrl Pts',(-20.7688588159742,19.8019488125389,
1.32323618964279));
#193753=CARTESIAN_POINT('Ctrl Pts',(-20.735559598103,19.9006641156182,1.32934395282682));
#193754=CARTESIAN_POINT('Ctrl Pts',(-20.7310458706774,19.913627350948,1.33015272451101));
#193755=CARTESIAN_POINT('Ctrl Pts',(-20.7251405246782,19.9300705383681,
1.33118747866683));
#193756=CARTESIAN_POINT('Ctrl Pts',(-20.7238652303846,19.9335921343837,
1.33140960977109));
#193757=CARTESIAN_POINT('Ctrl Pts',(-20.7225806064482,19.93711030268,1.33163204998037));
#193758=CARTESIAN_POINT('Origin',(-18.734,19.211,0.));
#193759=CARTESIAN_POINT('',(-20.7225806064941,19.9371103025544,2.35747633162257));
#193760=CARTESIAN_POINT('',(-20.7227695185423,19.9371792543491,2.1335156684528));
#193761=CARTESIAN_POINT('',(-20.7225806064498,19.9371103026755,0.));
#193762=CARTESIAN_POINT('Ctrl Pts',(-20.7225806064941,19.9371103025544,
2.35747633162257));
#193763=CARTESIAN_POINT('Ctrl Pts',(-20.7258083370006,19.9282705956041,
2.35692307432503));
#193764=CARTESIAN_POINT('Ctrl Pts',(-20.7289770874423,19.9194094713397,
2.35636790109843));
#193765=CARTESIAN_POINT('Ctrl Pts',(-20.7349196690319,19.9024354529302,
2.35530318962104));
#193766=CARTESIAN_POINT('Ctrl Pts',(-20.7377034729521,19.8943263471203,
2.35479399943749));
#193767=CARTESIAN_POINT('Ctrl Pts',(-20.7424958166832,19.8800853356252,
2.35389873934373));
#193768=CARTESIAN_POINT('Ctrl Pts',(-20.744525736348,19.8739607032413,2.35351338181118));
#193769=CARTESIAN_POINT('Ctrl Pts',(-20.7484115459079,19.8620545243679,
2.35276356970637));
#193770=CARTESIAN_POINT('Ctrl Pts',(-20.7502706246368,19.8562740789923,
2.35239922471625));
#193771=CARTESIAN_POINT('Ctrl Pts',(-20.7546531726338,19.8424435269296,
2.35152669771869));
#193772=CARTESIAN_POINT('Ctrl Pts',(-20.7571534259374,19.8343862235171,
2.35101775858528));
#193773=CARTESIAN_POINT('Ctrl Pts',(-20.7659891992941,19.8052989895712,
2.34917807743202));
#193774=CARTESIAN_POINT('Ctrl Pts',(-20.7720453452344,19.7841862775621,
2.34783825951628));
#193775=CARTESIAN_POINT('Ctrl Pts',(-20.8265422866132,19.5824062340106,
2.33498643421796));
#193776=CARTESIAN_POINT('Ctrl Pts',(-20.851156347104,19.3961933090496,2.32266067027536));
#193777=CARTESIAN_POINT('Ctrl Pts',(-20.8509463100805,19.1462094374975,
2.30615866168918));
#193778=CARTESIAN_POINT('Ctrl Pts',(-20.8480800911786,19.0832283197751,
2.30201616600222));
#193779=CARTESIAN_POINT('Ctrl Pts',(-20.837918860491,18.9707861185551,2.29473641728172));
#193780=CARTESIAN_POINT('Ctrl Pts',(-20.8316744047912,18.9212755815429,
2.29157206213904));
#193781=CARTESIAN_POINT('Ctrl Pts',(-20.8224344768722,18.8643135220372,
2.28801331259313));
#193782=CARTESIAN_POINT('Ctrl Pts',(-20.8211403746173,18.8566059549827,
2.28753352859736));
#193783=CARTESIAN_POINT('Ctrl Pts',(-20.8190058160593,18.844310073383,2.28677112202291));
#193784=CARTESIAN_POINT('Ctrl Pts',(-20.818192841526,18.8397171488273,2.28648700577087));
#193785=CARTESIAN_POINT('Ctrl Pts',(-20.8167271896738,18.8315934302223,
2.28598570510313));
#193786=CARTESIAN_POINT('Ctrl Pts',(-20.8160807012362,18.8280615635935,
2.28576817293963));
#193787=CARTESIAN_POINT('Ctrl Pts',(-20.8146926431108,18.8205858247794,
2.28530862225324));
#193788=CARTESIAN_POINT('Ctrl Pts',(-20.8139488460956,18.8166424191797,
2.28506673215675));
#193789=CARTESIAN_POINT('Ctrl Pts',(-20.8119140363715,18.8060203361484,
2.28441651366059));
#193790=CARTESIAN_POINT('Ctrl Pts',(-20.810602027063,18.7993456610807,2.28400936519241));
#193791=CARTESIAN_POINT('Ctrl Pts',(-20.803970729535,18.7664484432482,2.28200923301305));
#193792=CARTESIAN_POINT('Ctrl Pts',(-20.7981865505351,18.7403207641232,
2.28044128843594));
#193793=CARTESIAN_POINT('Ctrl Pts',(-20.7800922310083,18.6653518059024,
2.27598366438792));
#193794=CARTESIAN_POINT('Ctrl Pts',(-20.7665321461988,18.6168290476827,
2.27314937726003));
#193795=CARTESIAN_POINT('Ctrl Pts',(-20.7111897277366,18.4429806428975,
2.26303185761288));
#193796=CARTESIAN_POINT('Ctrl Pts',(-20.6594360217855,18.3211508442493,
2.25599591422191));
#193797=CARTESIAN_POINT('Ctrl Pts',(-20.547245161614,18.1134367048173,2.24300921728127));
#193798=CARTESIAN_POINT('Ctrl Pts',(-20.4911568897142,18.0257157213685,
2.23716710359459));
#193799=CARTESIAN_POINT('Ctrl Pts',(-20.4204318607925,17.931221022007,2.23025035766843));
#193800=CARTESIAN_POINT('Ctrl Pts',(-20.4118958788883,17.9200499393819,
2.22942226593358));
#193801=CARTESIAN_POINT('Ctrl Pts',(-20.398090742884,17.9023513264738,2.22809315366176));
#193802=CARTESIAN_POINT('Ctrl Pts',(-20.3928928708287,17.8957685407889,
2.22759495475064));
#193803=CARTESIAN_POINT('Ctrl Pts',(-20.3836314072036,17.8841817112644,
2.22671111081189));
#193804=CARTESIAN_POINT('Ctrl Pts',(-20.3795837997856,17.8791649849098,
2.22632610981205));
#193805=CARTESIAN_POINT('Ctrl Pts',(-20.3711396549156,17.86879631854,2.22552550100565));
#193806=CARTESIAN_POINT('Ctrl Pts',(-20.3667396432207,17.8634473190618,
2.2251097551417));
#193807=CARTESIAN_POINT('Ctrl Pts',(-20.3553245529637,17.849708224409,2.22403477989301));
#193808=CARTESIAN_POINT('Ctrl Pts',(-20.3482706313711,17.8413508018482,
2.22337396825025));
#193809=CARTESIAN_POINT('Ctrl Pts',(-20.3180882580626,17.8061480577944,
2.22056073146907));
#193810=CARTESIAN_POINT('Ctrl Pts',(-20.2943535738347,17.7798322686497,
2.21838329754759));
#193811=CARTESIAN_POINT('Ctrl Pts',(-20.2303134845433,17.7123153230627,
2.2125935812829));
#193812=CARTESIAN_POINT('Ctrl Pts',(-20.188968672702,17.672144894414,2.20893873669524));
#193813=CARTESIAN_POINT('Ctrl Pts',(-20.0462318762339,17.5443621398683,
2.19660000518597));
#193814=CARTESIAN_POINT('Ctrl Pts',(-19.9381729687711,17.4646905791544,
2.18767359816132));
#193815=CARTESIAN_POINT('Ctrl Pts',(-19.746372921014,17.3495908055372,2.17297280290509));
#193816=CARTESIAN_POINT('Ctrl Pts',(-19.6665527342797,17.3083459893408,
2.16715227537536));
#193817=CARTESIAN_POINT('Ctrl Pts',(-19.5755079983687,17.2684124357765,
2.16101027401375));
#193818=CARTESIAN_POINT('Ctrl Pts',(-19.5666425089598,17.2645959781263,
2.16041727244592));
#193819=CARTESIAN_POINT('Ctrl Pts',(-19.5535033404576,17.2590459694984,
2.159546224005));
#193820=CARTESIAN_POINT('Ctrl Pts',(-19.54924974574,17.2572655975766,2.15926543943138));
#193821=CARTESIAN_POINT('Ctrl Pts',(-19.5416882442493,17.2541296723596,
2.15876847387096));
#193822=CARTESIAN_POINT('Ctrl Pts',(-19.5383826912116,17.2527685872574,
2.15855196085396));
#193823=CARTESIAN_POINT('Ctrl Pts',(-19.5312874481935,17.2498680677301,
2.1580888148879));
#193824=CARTESIAN_POINT('Ctrl Pts',(-19.5274967503697,17.2483312458238,
2.15784234010848));
#193825=CARTESIAN_POINT('Ctrl Pts',(-19.5170660112718,17.244137582312,2.15716671059019));
#193826=CARTESIAN_POINT('Ctrl Pts',(-19.5104168530839,17.2415033582937,
2.15673889927245));
#193827=CARTESIAN_POINT('Ctrl Pts',(-19.474642028307,17.227539630704,2.15445187227512));
#193828=CARTESIAN_POINT('Ctrl Pts',(-19.4452798811727,17.216821769449,2.15262712912745));
#193829=CARTESIAN_POINT('Ctrl Pts',(-19.2606290852214,17.1540177449465,
2.14141264561027));
#193830=CARTESIAN_POINT('Ctrl Pts',(-19.0999557970955,17.1194448667353,
2.1327577596003));
#193831=CARTESIAN_POINT('Ctrl Pts',(-18.8202504340664,17.0925146077549,
2.11737625119989));
#193832=CARTESIAN_POINT('Ctrl Pts',(-18.7028972266081,17.0909889580431,
2.11083589061962));
#193833=CARTESIAN_POINT('Ctrl Pts',(-18.5717696855549,17.1001767824266,
2.10313521104301));
#193834=CARTESIAN_POINT('Ctrl Pts',(-18.5575209690726,17.1013202926768,
2.10229343993255));
#193835=CARTESIAN_POINT('Ctrl Pts',(-18.5348635434246,17.1033697724834,
2.10094651766514));
#193836=CARTESIAN_POINT('Ctrl Pts',(-18.5264466412293,17.1041819954307,
2.10044431007719));
#193837=CARTESIAN_POINT('Ctrl Pts',(-18.511611565799,17.1057033278525,2.09955580802749));
#193838=CARTESIAN_POINT('Ctrl Pts',(-18.5051913115994,17.106391419739,2.09917018002476));
#193839=CARTESIAN_POINT('Ctrl Pts',(-18.4919194249586,17.1078752836032,
2.09837068351477));
#193840=CARTESIAN_POINT('Ctrl Pts',(-18.4850683404699,17.1086751904943,
2.0979566888701));
#193841=CARTESIAN_POINT('Ctrl Pts',(-18.4674939994984,17.1108142147692,
2.09689135437236));
#193842=CARTESIAN_POINT('Ctrl Pts',(-18.4567769632541,17.1122019721029,
2.09623848599041));
#193843=CARTESIAN_POINT('Ctrl Pts',(-18.4121029017266,17.1183349890723,
2.09350327361417));
#193844=CARTESIAN_POINT('Ctrl Pts',(-18.3782546107007,17.123822577768,2.09139761636602));
#193845=CARTESIAN_POINT('Ctrl Pts',(-18.2904310993027,17.1402591315567,
2.08584401235039));
#193846=CARTESIAN_POINT('Ctrl Pts',(-18.2367260837093,17.1524959444146,
2.08235769518531));
#193847=CARTESIAN_POINT('Ctrl Pts',(-18.0779619843425,17.1952462599452,
2.07178963441209));
#193848=CARTESIAN_POINT('Ctrl Pts',(-17.9747307892796,17.2318194075763,
2.06455949505509));
#193849=CARTESIAN_POINT('Ctrl Pts',(-17.8336072438721,17.2944893896417,
2.0543593205525));
#193850=CARTESIAN_POINT('Ctrl Pts',(-17.7930125337472,17.3140912502936,
2.05138771895395));
#193851=CARTESIAN_POINT('Ctrl Pts',(-17.7315241471326,17.3462419712409,
2.04685423655292));
#193852=CARTESIAN_POINT('Ctrl Pts',(-17.7101698028667,17.3578804322822,
2.04527363202804));
#193853=CARTESIAN_POINT('Ctrl Pts',(-17.6764698715496,17.3770078301368,
2.04277421216629));
#193854=CARTESIAN_POINT('Ctrl Pts',(-17.6639924591252,17.3842594241168,
2.04184768595572));
#193855=CARTESIAN_POINT('Ctrl Pts',(-17.619633958912,17.4106500449378,2.03855222127833));
#193856=CARTESIAN_POINT('Ctrl Pts',(-17.5881821264162,17.4305019170751,
2.03621261754915));
#193857=CARTESIAN_POINT('Ctrl Pts',(-17.5513103956448,17.4551567114566,
2.03348106413737));
#193858=CARTESIAN_POINT('Ctrl Pts',(-17.545373434595,17.4591703149171,2.03304159686524));
#193859=CARTESIAN_POINT('Ctrl Pts',(-17.5357254037224,17.465764365517,2.03232816526987));
#193860=CARTESIAN_POINT('Ctrl Pts',(-17.5320020716161,17.4683266487978,
2.03205302092957));
#193861=CARTESIAN_POINT('Ctrl Pts',(-17.5253553732641,17.4729321398766,
2.03156221327305));
#193862=CARTESIAN_POINT('Ctrl Pts',(-17.5224289481114,17.4749708219706,
2.03134624923917));
#193863=CARTESIAN_POINT('Ctrl Pts',(-17.5161064391476,17.4793991460541,
2.03087994899954));
#193864=CARTESIAN_POINT('Ctrl Pts',(-17.5127122405319,17.4817913797909,
2.03062979391265));
#193865=CARTESIAN_POINT('Ctrl Pts',(-17.5032605254076,17.4884946666344,
2.02993361865172));
#193866=CARTESIAN_POINT('Ctrl Pts',(-17.4972185795621,17.4928277153981,
2.02948908081139));
#193867=CARTESIAN_POINT('Ctrl Pts',(-17.4624473827256,17.5180427195761,
2.0269328177355));
#193868=CARTESIAN_POINT('Ctrl Pts',(-17.4342225954955,17.5396145131729,
2.02486588513897));
#193869=CARTESIAN_POINT('Ctrl Pts',(-17.3455905585501,17.6109585959089,
2.01835413227576));
#193870=CARTESIAN_POINT('Ctrl Pts',(-17.2873918049756,17.6633760446575,
2.01404431440661));
#193871=CARTESIAN_POINT('Ctrl Pts',(-17.0993857698685,17.8526010146753,
1.99949369086041));
#193872=CARTESIAN_POINT('Ctrl Pts',(-16.9850088288275,18.0034257238715,
1.98942786273719));
#193873=CARTESIAN_POINT('Ctrl Pts',(-16.8813546360488,18.1863684794536,
1.97719494500122));
#193874=CARTESIAN_POINT('Ctrl Pts',(-16.8708981147763,18.2055071305123,
1.97591627478501));
#193875=CARTESIAN_POINT('Ctrl Pts',(-16.8568209136995,18.2322464906009,
1.97412983086024));
#193876=CARTESIAN_POINT('Ctrl Pts',(-16.8529468629093,18.2397127888505,
1.97363101752833));
#193877=CARTESIAN_POINT('Ctrl Pts',(-16.8463560133552,18.2526023942967,
1.97276980516306));
#193878=CARTESIAN_POINT('Ctrl Pts',(-16.8436178184557,18.2580146918992,
1.97240816274895));
#193879=CARTESIAN_POINT('Ctrl Pts',(-16.8380133321823,18.2692116833683,
1.97165991337662));
#193880=CARTESIAN_POINT('Ctrl Pts',(-16.8351501694008,18.2749978646993,
1.97127320176178));
#193881=CARTESIAN_POINT('Ctrl Pts',(-16.8285363522481,18.2885190063735,
1.97036938717927));
#193882=CARTESIAN_POINT('Ctrl Pts',(-16.824806275711,18.2962638543073,1.96985157431136));
#193883=CARTESIAN_POINT('Ctrl Pts',(-16.8129678213732,18.321232187129,1.9681817330836));
#193884=CARTESIAN_POINT('Ctrl Pts',(-16.8050447309268,18.3385420211256,
1.96702333482139));
#193885=CARTESIAN_POINT('Ctrl Pts',(-16.7663604989393,18.4261603951531,
1.96115449531175));
#193886=CARTESIAN_POINT('Ctrl Pts',(-16.7392083718904,18.4979905446274,
1.95632311388193));
#193887=CARTESIAN_POINT('Ctrl Pts',(-16.6826152379122,18.6764703364228,
1.94428019424811));
#193888=CARTESIAN_POINT('Ctrl Pts',(-16.6575151682528,18.7842580782506,
1.93696891770298));
#193889=CARTESIAN_POINT('Ctrl Pts',(-16.6298780378241,18.9664517725166,
1.92479845314424));
#193890=CARTESIAN_POINT('Ctrl Pts',(-16.6226329904922,19.03993392899,1.91994307867057));
#193891=CARTESIAN_POINT('Ctrl Pts',(-16.6172136150019,19.1576578260206,
1.91237655293546));
#193892=CARTESIAN_POINT('Ctrl Pts',(-16.6165617923873,19.2017240223307,
1.90959198699267));
#193893=CARTESIAN_POINT('Ctrl Pts',(-16.6174096716781,19.2533234549422,
1.90641127088156));
#193894=CARTESIAN_POINT('Ctrl Pts',(-16.6175739039016,19.2608645809207,
1.90594842080259));
#193895=CARTESIAN_POINT('Ctrl Pts',(-16.6179027442007,19.2729872428002,
1.90520776627002));
#193896=CARTESIAN_POINT('Ctrl Pts',(-16.618041933233,19.2775693237704,1.90492859644079));
#193897=CARTESIAN_POINT('Ctrl Pts',(-16.6183163360682,19.2857291935196,
1.90443287796156));
#193898=CARTESIAN_POINT('Ctrl Pts',(-16.6184457434308,19.2893071287099,
1.90421600834757));
#193899=CARTESIAN_POINT('Ctrl Pts',(-16.6187412494184,19.2969412444764,
1.90375434411372));
#193900=CARTESIAN_POINT('Ctrl Pts',(-16.6189099377581,19.3009972702751,
1.90350969598839));
#193901=CARTESIAN_POINT('Ctrl Pts',(-16.6194018272902,19.3120580964329,
1.90284421015918));
#193902=CARTESIAN_POINT('Ctrl Pts',(-16.6197481696241,19.319061888617,1.90242464952712));
#193903=CARTESIAN_POINT('Ctrl Pts',(-16.621725355079,19.3553852954967,1.90025760287986));
#193904=CARTESIAN_POINT('Ctrl Pts',(-16.6239313900089,19.3846719507194,
1.8985404494388));
#193905=CARTESIAN_POINT('Ctrl Pts',(-16.6322961696378,19.471543772585,1.89351153264984));
#193906=CARTESIAN_POINT('Ctrl Pts',(-16.6402090956601,19.5289349739786,
1.89027357571878));
#193907=CARTESIAN_POINT('Ctrl Pts',(-16.6798591510338,19.7492735420975,
1.87793081563257));
#193908=CARTESIAN_POINT('Ctrl Pts',(-16.7283560757306,19.9085865619674,
1.86914773812102));
#193909=CARTESIAN_POINT('Ctrl Pts',(-16.8200857739345,20.1179398975091,
1.85628654995288));
#193910=CARTESIAN_POINT('Ctrl Pts',(-16.8477370071711,20.1741295246211,
1.85269839702926));
#193911=CARTESIAN_POINT('Ctrl Pts',(-16.8838245483546,20.239929024275,1.8482909681105));
#193912=CARTESIAN_POINT('Ctrl Pts',(-16.8899102150147,20.2507966117704,
1.84755612672559));
#193913=CARTESIAN_POINT('Ctrl Pts',(-16.9000594582229,20.2685514280333,
1.84634390960961));
#193914=CARTESIAN_POINT('Ctrl Pts',(-16.9040668384881,20.2754705516952,
1.84586855853382));
#193915=CARTESIAN_POINT('Ctrl Pts',(-16.9113411678317,20.2878678951228,
1.84501146244165));
#193916=CARTESIAN_POINT('Ctrl Pts',(-16.9145938740788,20.2933543918753,
1.84463023834275));
#193917=CARTESIAN_POINT('Ctrl Pts',(-16.9215732617618,20.3050064994763,
1.84381647882346));
#193918=CARTESIAN_POINT('Ctrl Pts',(-16.9253067145432,20.3111679415082,
1.84338369887726));
#193919=CARTESIAN_POINT('Ctrl Pts',(-16.9354432966271,20.3277056238536,
1.84221533561125));
#193920=CARTESIAN_POINT('Ctrl Pts',(-16.9419046666353,20.3380456831811,
1.84147761428908));
#193921=CARTESIAN_POINT('Ctrl Pts',(-16.9746227203249,20.3894112522024,
1.83777619086537));
#193922=CARTESIAN_POINT('Ctrl Pts',(-17.0021987043686,20.4295750494239,
1.83476357395853));
#193923=CARTESIAN_POINT('Ctrl Pts',(-17.0856179040998,20.5425162462129,
1.82593647662104));
#193924=CARTESIAN_POINT('Ctrl Pts',(-17.1448321631763,20.6126566642694,
1.82000152537663));
#193925=CARTESIAN_POINT('Ctrl Pts',(-17.2753410281926,20.7483110795851,
1.80763880285383));
#193926=CARTESIAN_POINT('Ctrl Pts',(-17.3469621728779,20.8132288390426,
1.80121568213012));
#193927=CARTESIAN_POINT('Ctrl Pts',(-17.4836221018539,20.9210447851366,
1.78982360829918));
#193928=CARTESIAN_POINT('Ctrl Pts',(-17.5470790787152,20.9656850037643,
1.78482798822033));
#193929=CARTESIAN_POINT('Ctrl Pts',(-17.620917434964,21.0117850201804,1.77945151558655));
#193930=CARTESIAN_POINT('Ctrl Pts',(-17.6290203626898,21.0167683944472,
1.77886718027165));
#193931=CARTESIAN_POINT('Ctrl Pts',(-17.6410774151889,21.0240720436402,
1.77800638864554));
#193932=CARTESIAN_POINT('Ctrl Pts',(-17.6450057994789,21.0264342852233,
1.77772728505667));
#193933=CARTESIAN_POINT('Ctrl Pts',(-17.6520090689725,21.0306146253844,
1.77723216947439));
#193934=CARTESIAN_POINT('Ctrl Pts',(-17.6550809077026,21.0324377158368,
1.77701583476367));
#193935=CARTESIAN_POINT('Ctrl Pts',(-17.6616953844734,21.036340704356,1.77655181559128));
#193936=CARTESIAN_POINT('Ctrl Pts',(-17.6652394558983,21.0384180625925,
1.77630429589092));
#193937=CARTESIAN_POINT('Ctrl Pts',(-17.6750393388708,21.0441240053895,
1.77562284658762));
#193938=CARTESIAN_POINT('Ctrl Pts',(-17.6813077994382,21.0477309098678,
1.77519029914606));
#193939=CARTESIAN_POINT('Ctrl Pts',(-17.7157565007453,21.0673185812155,
1.77283076321627));
#193940=CARTESIAN_POINT('Ctrl Pts',(-17.744283887119,21.0826839405927,1.77094088613304));
#193941=CARTESIAN_POINT('Ctrl Pts',(-17.9182188363299,21.1712789194842,
1.7597315590692));
#193942=CARTESIAN_POINT('Ctrl Pts',(-18.07133709615,21.2281965990321,1.75112687495386));
#193943=CARTESIAN_POINT('Ctrl Pts',(-18.3429908796731,21.2948573269123,
1.73581422361014));
#193944=CARTESIAN_POINT('Ctrl Pts',(-18.4585978772053,21.3132601876843,
1.72928959262602));
#193945=CARTESIAN_POINT('Ctrl Pts',(-18.5893741822905,21.3231024106734,
1.72160661815243));
#193946=CARTESIAN_POINT('Ctrl Pts',(-18.6036346747824,21.3240305457778,
1.72076507144283));
#193947=CARTESIAN_POINT('Ctrl Pts',(-18.6263453904664,21.3252778838986,
1.71941844131572));
#193948=CARTESIAN_POINT('Ctrl Pts',(-18.634790171541,21.3256909684562,1.71891629945182));
#193949=CARTESIAN_POINT('Ctrl Pts',(-18.6496880282078,21.3263302773831,
1.71802787415162));
#193950=CARTESIAN_POINT('Ctrl Pts',(-18.6561401248943,21.3265775876635,
1.71764225680737));
#193951=CARTESIAN_POINT('Ctrl Pts',(-18.6694873680134,21.3270280489729,
1.71684274358255));
#193952=CARTESIAN_POINT('Ctrl Pts',(-18.6763825702282,21.3272270232091,
1.71642872137321));
#193953=CARTESIAN_POINT('Ctrl Pts',(-18.6940840311506,21.3276512562827,
1.71536323420402));
#193954=CARTESIAN_POINT('Ctrl Pts',(-18.7048911673507,21.3278274597541,
1.71471023986695));
#193955=CARTESIAN_POINT('Ctrl Pts',(-18.7500025742677,21.328217452008,1.71197380483497));
#193956=CARTESIAN_POINT('Ctrl Pts',(-18.7843065669613,21.3276801493136,
1.70986702479858));
#193957=CARTESIAN_POINT('Ctrl Pts',(-18.8736412130645,21.3241080950453,
1.70430975168817));
#193958=CARTESIAN_POINT('Ctrl Pts',(-18.9285905010767,21.3197577399365,
1.70082082497084));
#193959=CARTESIAN_POINT('Ctrl Pts',(-19.0871715552301,21.3009519218248,
1.69055625303314));
#193960=CARTESIAN_POINT('Ctrl Pts',(-19.1899762856936,21.2809545168195,
1.68365003757954));
#193961=CARTESIAN_POINT('Ctrl Pts',(-19.4098718339464,21.2209998733261,
1.66858985106));
#193962=CARTESIAN_POINT('Ctrl Pts',(-19.5258210272218,21.17821342418,1.66046083813723));
#193963=CARTESIAN_POINT('Ctrl Pts',(-19.6459306174739,21.1215393591917,
1.65225901090985));
#193964=CARTESIAN_POINT('Ctrl Pts',(-19.6544401566968,21.117454305677,1.65167924091008));
#193965=CARTESIAN_POINT('Ctrl Pts',(-19.6670283199641,21.1113073525025,
1.65082385770607));
#193966=CARTESIAN_POINT('Ctrl Pts',(-19.6711279142617,21.1092890067232,
1.65054564431789));
#193967=CARTESIAN_POINT('Ctrl Pts',(-19.6784194143644,21.1056698182203,
1.65005150168731));
#193968=CARTESIAN_POINT('Ctrl Pts',(-19.6816138289532,21.104074161814,1.64983525468109));
#193969=CARTESIAN_POINT('Ctrl Pts',(-19.6884093605998,21.1006581842282,
1.64937574297494));
#193970=CARTESIAN_POINT('Ctrl Pts',(-19.692009302844,21.0988356541581,1.64913261959681));
#193971=CARTESIAN_POINT('Ctrl Pts',(-19.7018354092485,21.0938256809191,
1.64846978133991));
#193972=CARTESIAN_POINT('Ctrl Pts',(-19.7080510864723,21.0906176228627,
1.64805134043633));
#193973=CARTESIAN_POINT('Ctrl Pts',(-19.7219080525441,21.083378517952,1.6471201345054));
#193974=CARTESIAN_POINT('Ctrl Pts',(-19.7295408395043,21.0793313617043,
1.64660832929403));
#193975=CARTESIAN_POINT('Ctrl Pts',(-19.752995588107,21.0667103291821,1.64503843378264));
#193976=CARTESIAN_POINT('Ctrl Pts',(-19.7687335679533,21.0579811373214,
1.64398903592947));
#193977=CARTESIAN_POINT('Ctrl Pts',(-19.828886429719,21.0236066531205,1.6399861360298));
#193978=CARTESIAN_POINT('Ctrl Pts',(-19.8724777658955,20.9965498472194,
1.63710225204504));
#193979=CARTESIAN_POINT('Ctrl Pts',(-20.0283803324946,20.8917490819468,
1.62669288391142));
#193980=CARTESIAN_POINT('Ctrl Pts',(-20.1340789811193,20.804775142282,1.61942670334326));
#193981=CARTESIAN_POINT('Ctrl Pts',(-20.3002696004928,20.6386463557276,
1.60646865982797));
#193982=CARTESIAN_POINT('Ctrl Pts',(-20.3649281372122,20.5643087019784,
1.60092488104402));
#193983=CARTESIAN_POINT('Ctrl Pts',(-20.43257196273,20.4746204378556,1.5943407417292));
#193984=CARTESIAN_POINT('Ctrl Pts',(-20.4408556345718,20.4634085405383,
1.59351955992391));
#193985=CARTESIAN_POINT('Ctrl Pts',(-20.4539248015979,20.4453489974257,
1.5921994494648));
#193986=CARTESIAN_POINT('Ctrl Pts',(-20.4587816277087,20.4385532999689,
1.59170328170978));
#193987=CARTESIAN_POINT('Ctrl Pts',(-20.4673119154711,20.4264671057377,
1.59082178566523));
#193988=CARTESIAN_POINT('Ctrl Pts',(-20.4710017095797,20.4211882254205,
1.59043709005023));
#193989=CARTESIAN_POINT('Ctrl Pts',(-20.4786180162605,20.4101852067226,
1.58963586225675));
#193990=CARTESIAN_POINT('Ctrl Pts',(-20.482540574539,20.4044584366823,1.58921918581006));
#193991=CARTESIAN_POINT('Ctrl Pts',(-20.4926090908109,20.3896026374459,
1.58813910720564));
#193992=CARTESIAN_POINT('Ctrl Pts',(-20.4987120973301,20.3804448758496,
1.58747409412736));
#193993=CARTESIAN_POINT('Ctrl Pts',(-20.5245036292371,20.3410821749285,
1.584618735998));
#193994=CARTESIAN_POINT('Ctrl Pts',(-20.5434892339324,20.3104259546805,
1.58240244054529));
#193995=CARTESIAN_POINT('Ctrl Pts',(-20.5914724005276,20.2283349139736,
1.57648346236878));
#193996=CARTESIAN_POINT('Ctrl Pts',(-20.619115622545,20.1761487659913,1.57273581705888));
#193997=CARTESIAN_POINT('Ctrl Pts',(-20.6735090116571,20.0621854787197,
1.5645939701441));
#193998=CARTESIAN_POINT('Ctrl Pts',(-20.6995477912786,20.0001897629222,
1.56018956835498));
#193999=CARTESIAN_POINT('Ctrl Pts',(-20.7225807924205,19.937109793362,1.55576067791233));
#194000=CARTESIAN_POINT('',(-20.8479202339018,19.2101717420009,2.08900081873324));
#194001=CARTESIAN_POINT('Ctrl Pts',(-20.7225806064482,19.93711030268,1.33163204998037));
#194002=CARTESIAN_POINT('Ctrl Pts',(-20.7210219801323,19.9413788746215,
1.33190193531729));
#194003=CARTESIAN_POINT('Ctrl Pts',(-20.7194496198182,19.9456424006789,
1.33217227569476));
#194004=CARTESIAN_POINT('Ctrl Pts',(-20.7156191794292,19.9559266917663,
1.33282626855238));
#194005=CARTESIAN_POINT('Ctrl Pts',(-20.7133473849464,19.9619422592217,
1.33321037582342));
#194006=CARTESIAN_POINT('Ctrl Pts',(-20.7085566179748,19.9744551210761,
1.33401266450812));
#194007=CARTESIAN_POINT('Ctrl Pts',(-20.7060329042928,19.9809505062436,
1.33443100152553));
#194008=CARTESIAN_POINT('Ctrl Pts',(-20.6993949396819,19.9977881672302,
1.33552036370451));
#194009=CARTESIAN_POINT('Ctrl Pts',(-20.69523115058,20.0081105667363,1.33619305310805));
#194010=CARTESIAN_POINT('Ctrl Pts',(-20.6767885689131,20.0528119545002,
1.33912762571572));
#194011=CARTESIAN_POINT('Ctrl Pts',(-20.6616864783648,20.086842083609,1.34141728728153));
#194012=CARTESIAN_POINT('Ctrl Pts',(-20.619174301263,20.1762037026226,1.34758328748549));
#194013=CARTESIAN_POINT('Ctrl Pts',(-20.5902290357626,20.2307612337437,
1.35150939858986));
#194014=CARTESIAN_POINT('Ctrl Pts',(-20.4847193863011,20.4102152056578,
1.36495843768551));
#194015=CARTESIAN_POINT('Ctrl Pts',(-20.3975968400093,20.528412548849,1.37476366490735));
#194016=CARTESIAN_POINT('Ctrl Pts',(-20.2858390406964,20.6510922783274,
1.38559624225933));
#194017=CARTESIAN_POINT('Ctrl Pts',(-20.2724917414562,20.66534293502,1.3868651468458));
#194018=CARTESIAN_POINT('Ctrl Pts',(-20.2223171049878,20.7174495703338,
1.39153861523857));
#194019=CARTESIAN_POINT('Ctrl Pts',(-20.1842710771645,20.7541114429139,
1.39489478220167));
#194020=CARTESIAN_POINT('Ctrl Pts',(-20.1384093776391,20.7951082242178,
1.39868927155921));
#194021=CARTESIAN_POINT('Ctrl Pts',(-20.1318927159941,20.8008617947951,
1.39922279338419));
#194022=CARTESIAN_POINT('Ctrl Pts',(-20.1219663922015,20.8095175436712,
1.40002669898881));
#194023=CARTESIAN_POINT('Ctrl Pts',(-20.1185827513091,20.8124492339549,
1.40029920425877));
#194024=CARTESIAN_POINT('Ctrl Pts',(-20.1124893449964,20.8176949999569,
1.40078716852804));
#194025=CARTESIAN_POINT('Ctrl Pts',(-20.1097830276927,20.8200129764682,
1.40100291356046));
#194026=CARTESIAN_POINT('Ctrl Pts',(-20.1038860843768,20.8250379868895,
1.40147088500487));
#194027=CARTESIAN_POINT('Ctrl Pts',(-20.1006932920077,20.8277423893645,
1.4017229187453));
#194028=CARTESIAN_POINT('Ctrl Pts',(-20.0916937734164,20.8353195740922,
1.40242963365348));
#194029=CARTESIAN_POINT('Ctrl Pts',(-20.0858687956632,20.8401707167768,
1.40288275892046));
#194030=CARTESIAN_POINT('Ctrl Pts',(-20.0507099584497,20.8691331977841,
1.4055929180279));
#194031=CARTESIAN_POINT('Ctrl Pts',(-20.0207558051386,20.8924846766865,
1.40779861654323));
#194032=CARTESIAN_POINT('Ctrl Pts',(-19.919679264397,20.9669973916801,1.4149670293758));
#194033=CARTESIAN_POINT('Ctrl Pts',(-19.8460068841176,21.0145535140239,
1.4197614569395));
#194034=CARTESIAN_POINT('Ctrl Pts',(-19.6172786138434,21.1428401094856,
1.43402871201116));
#194035=CARTESIAN_POINT('Ctrl Pts',(-19.4549968073101,21.209085129227,1.44342161132237));
#194036=CARTESIAN_POINT('Ctrl Pts',(-19.2641710281374,21.2606680886938,
1.45490747645002));
#194037=CARTESIAN_POINT('Ctrl Pts',(-19.2418174444265,21.2663204067987,
1.45625818626721));
#194038=CARTESIAN_POINT('Ctrl Pts',(-19.2100739958543,21.2737975884584,
1.45818542731543));
#194039=CARTESIAN_POINT('Ctrl Pts',(-19.2007567509785,21.2759257786522,
1.45875220920406));
#194040=CARTESIAN_POINT('Ctrl Pts',(-19.1855974111556,21.2792805440006,
1.45967628392139));
#194041=CARTESIAN_POINT('Ctrl Pts',(-19.1797639105687,21.2805456422521,
1.46003233689495));
#194042=CARTESIAN_POINT('Ctrl Pts',(-19.167544176819,21.2831416461357,1.4607791698737));
#194043=CARTESIAN_POINT('Ctrl Pts',(-19.1611569949902,21.2844677366808,
1.46117009979784));
#194044=CARTESIAN_POINT('Ctrl Pts',(-19.1459516656235,21.2875513895421,
1.4621021350298));
#194045=CARTESIAN_POINT('Ctrl Pts',(-19.1371283024604,21.2892823234767,
1.46264408471871));
#194046=CARTESIAN_POINT('Ctrl Pts',(-19.1073848532958,21.2949207439661,
1.46447486056438));
#194047=CARTESIAN_POINT('Ctrl Pts',(-19.086417467998,21.298568871237,1.46577189765452));
#194048=CARTESIAN_POINT('Ctrl Pts',(-18.9080304550596,21.3268424920729,
1.47686494062663));
#194049=CARTESIAN_POINT('Ctrl Pts',(-18.7483780016142,21.3339345607675,
1.48723402128144));
#194050=CARTESIAN_POINT('Ctrl Pts',(-18.4581190095075,21.3140723894634,
1.50645220289788));
#194051=CARTESIAN_POINT('Ctrl Pts',(-18.3278779539579,21.2928488882342,
1.51519416249287));
#194052=CARTESIAN_POINT('Ctrl Pts',(-18.1852095922554,21.255692133338,1.52439164038815));
#194053=CARTESIAN_POINT('Ctrl Pts',(-18.1700193264239,21.2515544994403,
1.52536571578161));
#194054=CARTESIAN_POINT('Ctrl Pts',(-18.1492987512426,21.2456614148295,
1.52668594932913));
#194055=CARTESIAN_POINT('Ctrl Pts',(-18.1437278409085,21.2440522382159,
1.52704006298472));
#194056=CARTESIAN_POINT('Ctrl Pts',(-18.1348885921039,21.2414595954865,
1.5276005088182));
#194057=CARTESIAN_POINT('Ctrl Pts',(-18.1316159471186,21.2404910941394,
1.52780769856876));
#194058=CARTESIAN_POINT('Ctrl Pts',(-18.1248643571976,21.238475269468,1.52823447783236));
#194059=CARTESIAN_POINT('Ctrl Pts',(-18.1213857646962,21.2374269043043,
1.52845399909992));
#194060=CARTESIAN_POINT('Ctrl Pts',(-18.1131072948803,21.2349087053527,
1.52897558268967));
#194061=CARTESIAN_POINT('Ctrl Pts',(-18.1083098767027,21.2334307329704,
1.52927717034093));
#194062=CARTESIAN_POINT('Ctrl Pts',(-18.0921655107758,21.2283940873623,
1.530289951387));
#194063=CARTESIAN_POINT('Ctrl Pts',(-18.0808430656785,21.2247567998778,
1.53099669198937));
#194064=CARTESIAN_POINT('Ctrl Pts',(-17.9457581876221,21.1801021467023,
1.53939274105539));
#194065=CARTESIAN_POINT('Ctrl Pts',(-17.8259909109847,21.1278249250091,
1.54648533894591));
#194066=CARTESIAN_POINT('Ctrl Pts',(-17.5697567012959,20.9865368072029,
1.56238143050949));
#194067=CARTESIAN_POINT('Ctrl Pts',(-17.4372178433931,20.892172943223,1.5711604336109));
#194068=CARTESIAN_POINT('Ctrl Pts',(-17.2991282904203,20.7677257801433,
1.58195444034238));
#194069=CARTESIAN_POINT('Ctrl Pts',(-17.2817714598471,20.7515467139499,
1.58334382814564));
#194070=CARTESIAN_POINT('Ctrl Pts',(-17.2577302603234,20.7283694778242,
1.58531689758181));
#194071=CARTESIAN_POINT('Ctrl Pts',(-17.2508159379729,20.7216116343901,
1.58589018191496));
#194072=CARTESIAN_POINT('Ctrl Pts',(-17.2396938405766,20.710591268333,1.58682196063981));
#194073=CARTESIAN_POINT('Ctrl Pts',(-17.2354573881051,20.7063577864015,
1.58717917308321));
#194074=CARTESIAN_POINT('Ctrl Pts',(-17.226656353439,20.6974879622328,1.58792610575059));
#194075=CARTESIAN_POINT('Ctrl Pts',(-17.2220950719861,20.6928484463236,
1.5883159655961));
#194076=CARTESIAN_POINT('Ctrl Pts',(-17.2113471488286,20.6818148940398,
1.5892411921529));
#194077=CARTESIAN_POINT('Ctrl Pts',(-17.2051793219487,20.6754027752964,
1.58977737082846));
#194078=CARTESIAN_POINT('Ctrl Pts',(-17.1847748553258,20.6539207300488,
1.59156881988248));
#194079=CARTESIAN_POINT('Ctrl Pts',(-17.1707195237632,20.6386809471077,
1.59283182937378));
#194080=CARTESIAN_POINT('Ctrl Pts',(-17.0968888195151,20.5562308746983,
1.59962552830862));
#194081=CARTESIAN_POINT('Ctrl Pts',(-17.0412259293054,20.4854769397015,
1.60532414920766));
#194082=CARTESIAN_POINT('Ctrl Pts',(-16.9134494572044,20.2998630129998,
1.61992773361721));
#194083=CARTESIAN_POINT('Ctrl Pts',(-16.8475448694516,20.1812114728228,
1.62897837382845));
#194084=CARTESIAN_POINT('Ctrl Pts',(-16.7632447013434,19.9878630755169,
1.64277153526155));
#194085=CARTESIAN_POINT('Ctrl Pts',(-16.7367835348864,19.9170606157419,
1.64763344815371));
#194086=CARTESIAN_POINT('Ctrl Pts',(-16.7113186000928,19.8359312469652,
1.65288523437605));
#194087=CARTESIAN_POINT('Ctrl Pts',(-16.7085367006307,19.8268551287328,
1.653468338077));
#194088=CARTESIAN_POINT('Ctrl Pts',(-16.7045032143848,19.8133726197446,
1.6543276685691));
#194089=CARTESIAN_POINT('Ctrl Pts',(-16.703204770918,19.808980530025,1.65460652995822));
#194090=CARTESIAN_POINT('Ctrl Pts',(-16.7009191219284,19.801155826853,1.65510137735914));
#194091=CARTESIAN_POINT('Ctrl Pts',(-16.6999263418062,19.7977249018458,
1.65531768476355));
#194092=CARTESIAN_POINT('Ctrl Pts',(-16.6978096797043,19.7903400344377,
1.6557818254181));
#194093=CARTESIAN_POINT('Ctrl Pts',(-16.6966886322303,19.7863853381737,
1.65602949295948));
#194094=CARTESIAN_POINT('Ctrl Pts',(-16.6936239227215,19.7754527712034,
1.6567117762454));
#194095=CARTESIAN_POINT('Ctrl Pts',(-16.6917045229514,19.7684680757904,
1.65714500418878));
#194096=CARTESIAN_POINT('Ctrl Pts',(-16.6813531719808,19.7300284188622,
1.65951524848396));
#194097=CARTESIAN_POINT('Ctrl Pts',(-16.673611532173,19.6983901152728,1.66141475411808));
#194098=CARTESIAN_POINT('Ctrl Pts',(-16.631599073941,19.5077414685826,1.67262337897791));
#194099=CARTESIAN_POINT('Ctrl Pts',(-16.6150144979466,19.3453779231829,
1.68122065938082));
#194100=CARTESIAN_POINT('Ctrl Pts',(-16.6187508090477,19.0658798490546,
1.69652311335512));
#194101=CARTESIAN_POINT('Ctrl Pts',(-16.6299799312674,18.9494024320638,
1.70304537510243));
#194102=CARTESIAN_POINT('Ctrl Pts',(-16.6532984614773,18.8203923877595,
1.71072567854626));
#194103=CARTESIAN_POINT('Ctrl Pts',(-16.6559824232015,18.8063567809064,
1.71156718170344));
#194104=CARTESIAN_POINT('Ctrl Pts',(-16.6604801797896,18.7840620235293,
1.71291375121977));
#194105=CARTESIAN_POINT('Ctrl Pts',(-16.6622017480682,18.7757845583075,
1.71341587634892));
#194106=CARTESIAN_POINT('Ctrl Pts',(-16.6653254310486,18.7612042494906,
1.71430427736137));
#194107=CARTESIAN_POINT('Ctrl Pts',(-16.6667068923005,18.7548970567565,
1.71468988721356));
#194108=CARTESIAN_POINT('Ctrl Pts',(-16.6696238737885,18.7418648460967,
1.71548939009626));
#194109=CARTESIAN_POINT('Ctrl Pts',(-16.6711634515581,18.7351408236042,
1.71590340947901));
#194110=CARTESIAN_POINT('Ctrl Pts',(-16.6751997173664,18.7179003915304,
1.71696890022436));
#194111=CARTESIAN_POINT('Ctrl Pts',(-16.6777441101175,18.7073954565501,
1.71762190105234));
#194112=CARTESIAN_POINT('Ctrl Pts',(-16.6886997835749,18.6636308631386,
1.72035845384063));
#194113=CARTESIAN_POINT('Ctrl Pts',(-16.6978380839052,18.6305601819208,
1.72246534820482));
#194114=CARTESIAN_POINT('Ctrl Pts',(-16.7237398248229,18.5449819924262,
1.72802300836551));
#194115=CARTESIAN_POINT('Ctrl Pts',(-16.7417564684323,18.4928838198673,
1.73151221538506));
#194116=CARTESIAN_POINT('Ctrl Pts',(-16.8015456967986,18.3396347969966,
1.74208581381004));
#194117=CARTESIAN_POINT('Ctrl Pts',(-16.8491452091636,18.2409608757493,
1.74931858449843));
#194118=CARTESIAN_POINT('Ctrl Pts',(-16.9285005074288,18.1045619344368,
1.75974265669016));
#194119=CARTESIAN_POINT('Ctrl Pts',(-16.9542796738513,18.0635552702121,
1.76293490421929));
#194120=CARTESIAN_POINT('Ctrl Pts',(-16.9913642549095,18.0088259373301,
1.76724780316153));
#194121=CARTESIAN_POINT('Ctrl Pts',(-17.0014688803577,17.9943086829254,
1.7683970128548));
#194122=CARTESIAN_POINT('Ctrl Pts',(-17.0427753808773,17.9365220989961,
1.77298776232825));
#194123=CARTESIAN_POINT('Ctrl Pts',(-17.0754285061932,17.8943085900685,
1.77637885811053));
#194124=CARTESIAN_POINT('Ctrl Pts',(-17.1152365163026,17.8466797224422,
1.78020805360985));
#194125=CARTESIAN_POINT('Ctrl Pts',(-17.1208699462202,17.8400235335685,
1.78074325128853));
#194126=CARTESIAN_POINT('Ctrl Pts',(-17.1294617383259,17.8299981662177,
1.7815491945669));
#194127=CARTESIAN_POINT('Ctrl Pts',(-17.1323898605233,17.8266033588356,
1.78182207696204));
#194128=CARTESIAN_POINT('Ctrl Pts',(-17.1376650503803,17.8205265447025,
1.78231045455654));
#194129=CARTESIAN_POINT('Ctrl Pts',(-17.1400081157676,17.8178411523271,
1.78252623786829));
#194130=CARTESIAN_POINT('Ctrl Pts',(-17.1451139404862,17.8120190992982,
1.7829939863762));
#194131=CARTESIAN_POINT('Ctrl Pts',(-17.1478792022982,17.8088847100052,
1.78324576054905));
#194132=CARTESIAN_POINT('Ctrl Pts',(-17.155672242294,17.8001039555202,1.78395102770169));
#194133=CARTESIAN_POINT('Ctrl Pts',(-17.1607210687068,17.7944762383457,
1.78440297492255));
#194134=CARTESIAN_POINT('Ctrl Pts',(-17.1910744505373,17.761005064852,1.78709140166385));
#194135=CARTESIAN_POINT('Ctrl Pts',(-17.2170891566877,17.7338113017969,
1.78927749713153));
#194136=CARTESIAN_POINT('Ctrl Pts',(-17.3050623907025,17.6466274838278,
1.79635040381578));
#194137=CARTESIAN_POINT('Ctrl Pts',(-17.3699642977016,17.5897248801626,
1.80107399952186));
#194138=CARTESIAN_POINT('Ctrl Pts',(-17.5778061456249,17.428841162142,1.81537759309751));
#194139=CARTESIAN_POINT('Ctrl Pts',(-17.7304096845272,17.3386554312784,
1.82486619265082));
#194140=CARTESIAN_POINT('Ctrl Pts',(-17.9134545786712,17.2593547823782,
1.83645888797792));
#194141=CARTESIAN_POINT('Ctrl Pts',(-17.934621891721,17.2505897307822,1.8378011256653));
#194142=CARTESIAN_POINT('Ctrl Pts',(-17.9647922760009,17.2386665212445,
1.83971832511273));
#194143=CARTESIAN_POINT('Ctrl Pts',(-17.973681311151,17.235222846334,1.84028367620528));
#194144=CARTESIAN_POINT('Ctrl Pts',(-17.9881693161024,17.2297223400254,
1.84120604127702));
#194145=CARTESIAN_POINT('Ctrl Pts',(-17.9937543169603,17.2276289044716,
1.84156182445295));
#194146=CARTESIAN_POINT('Ctrl Pts',(-18.0054692936836,17.2232941339921,
1.84230859983847));
#194147=CARTESIAN_POINT('Ctrl Pts',(-18.0116009288726,17.221057493202,1.84269974420532));
#194148=CARTESIAN_POINT('Ctrl Pts',(-18.0262232058863,17.2158002043669,
1.84363323022021));
#194149=CARTESIAN_POINT('Ctrl Pts',(-18.0347229338106,17.2128053659475,
1.84417642341575));
#194150=CARTESIAN_POINT('Ctrl Pts',(-18.0634738043621,17.2028810431611,
1.84601587832944));
#194151=CARTESIAN_POINT('Ctrl Pts',(-18.0838103256414,17.196204611278,1.84732045807473));
#194152=CARTESIAN_POINT('Ctrl Pts',(-18.1954197622506,17.1614292166487,
1.85450128670511));
#194153=CARTESIAN_POINT('Ctrl Pts',(-18.2884010228921,17.139226277544,1.86056765281151));
#194154=CARTESIAN_POINT('Ctrl Pts',(-18.5505639581331,17.0950916987946,
1.87784520501006));
#194155=CARTESIAN_POINT('Ctrl Pts',(-18.7213642528363,17.0871935141841,
1.88934038074912));
#194156=CARTESIAN_POINT('Ctrl Pts',(-18.9278551191995,17.10257503266,1.90255504073256));
#194157=CARTESIAN_POINT('Ctrl Pts',(-18.9643760218696,17.1062522922644,
1.9048632364457));
#194158=CARTESIAN_POINT('Ctrl Pts',(-19.007864637526,17.1117767896868,1.90756276575745));
#194159=CARTESIAN_POINT('Ctrl Pts',(-19.0149395416,17.1127119111806,1.90800037641221));
#194160=CARTESIAN_POINT('Ctrl Pts',(-19.0264784023802,17.1142964610959,
1.90871140342267));
#194161=CARTESIAN_POINT('Ctrl Pts',(-19.0309451842789,17.1149244039595,
1.9089859868437));
#194162=CARTESIAN_POINT('Ctrl Pts',(-19.0389395101046,17.1160743186059,
1.90947619136222));
#194163=CARTESIAN_POINT('Ctrl Pts',(-19.0424677604797,17.1165909289878,
1.90969211004854));
#194164=CARTESIAN_POINT('Ctrl Pts',(-19.0501085124337,17.1177294233781,
1.91015876390807));
#194165=CARTESIAN_POINT('Ctrl Pts',(-19.0542204787161,17.1183545106066,
1.91040931553867));
#194166=CARTESIAN_POINT('Ctrl Pts',(-19.0657080617744,17.1201354667003,
1.91110771447887));
#194167=CARTESIAN_POINT('Ctrl Pts',(-19.0730795298178,17.1213182512444,
1.91155406405324));
#194168=CARTESIAN_POINT('Ctrl Pts',(-19.1159773692034,17.1284343701754,
1.91414184735344));
#194169=CARTESIAN_POINT('Ctrl Pts',(-19.1513562307166,17.1352349751963,
1.91623718646327));
#194170=CARTESIAN_POINT('Ctrl Pts',(-19.2647982224745,17.1600590509605,
1.92287977136236));
#194171=CARTESIAN_POINT('Ctrl Pts',(-19.3420213067432,17.181611514481,1.92728568404138));
#194172=CARTESIAN_POINT('Ctrl Pts',(-19.5935406000503,17.2674606282222,
1.94177388425946));
#194173=CARTESIAN_POINT('Ctrl Pts',(-19.7605673945307,17.3502719959322,
1.95170323443065));
#194174=CARTESIAN_POINT('Ctrl Pts',(-19.9329942577577,17.4661246233785,
1.96378511893577));
#194175=CARTESIAN_POINT('Ctrl Pts',(-19.9511416933849,17.4787346178818,
1.96508050629727));
#194176=CARTESIAN_POINT('Ctrl Pts',(-19.9759568881357,17.4965602614094,
1.96688661928272));
#194177=CARTESIAN_POINT('Ctrl Pts',(-19.9827961457548,17.5015355480619,
1.96738812047849));
#194178=CARTESIAN_POINT('Ctrl Pts',(-19.9944985900138,17.5101563145602,
1.96825273673944));
#194179=CARTESIAN_POINT('Ctrl Pts',(-19.9993762622033,17.513782025904,1.96861508126713));
#194180=CARTESIAN_POINT('Ctrl Pts',(-20.0092317980577,17.5211740252801,
1.96935124480031));
#194181=CARTESIAN_POINT('Ctrl Pts',(-20.0142087493364,17.5249414243735,
1.9697251051651));
#194182=CARTESIAN_POINT('Ctrl Pts',(-20.0257363123027,17.5337479015135,
1.97059598368412));
#194183=CARTESIAN_POINT('Ctrl Pts',(-20.0322741895855,17.5388034122657,
1.97109364834265));
#194184=CARTESIAN_POINT('Ctrl Pts',(-20.0459552464992,17.5495110890584,
1.9721430325731));
#194185=CARTESIAN_POINT('Ctrl Pts',(-20.0530918697995,17.5551713237902,
1.97269506840962));
#194186=CARTESIAN_POINT('Ctrl Pts',(-20.0719930252715,17.5703620461178,
1.97416961822842));
#194187=CARTESIAN_POINT('Ctrl Pts',(-20.0836920576686,17.5799728505687,
1.97509534458661));
#194188=CARTESIAN_POINT('Ctrl Pts',(-20.1190530954181,17.6096630706265,
1.9779339251842));
#194189=CARTESIAN_POINT('Ctrl Pts',(-20.142376745457,17.6301373164522,1.97986259971846));
#194190=CARTESIAN_POINT('Ctrl Pts',(-20.2893723186999,17.7650102287499,
1.99238949493841));
#194191=CARTESIAN_POINT('Ctrl Pts',(-20.3994497338085,17.8933013198049,
2.00357762924864));
#194192=CARTESIAN_POINT('Ctrl Pts',(-20.5482373928072,18.1155372990444,
2.02119561177938));
#194193=CARTESIAN_POINT('Ctrl Pts',(-20.5974955279141,18.2016017037933,
2.02764827953092));
#194194=CARTESIAN_POINT('Ctrl Pts',(-20.64476467428,18.2995388947264,2.03436721312591));
#194195=CARTESIAN_POINT('Ctrl Pts',(-20.6489187114157,18.3082988735037,
2.03496288620485));
#194196=CARTESIAN_POINT('Ctrl Pts',(-20.6549630915623,18.3212746828114,
2.03583709280972));
#194197=CARTESIAN_POINT('Ctrl Pts',(-20.6568999795341,18.3254685161823,
2.03611839220426));
#194198=CARTESIAN_POINT('Ctrl Pts',(-20.6603117270552,18.3329197556956,
2.03661592599245));
#194199=CARTESIAN_POINT('Ctrl Pts',(-20.6617920753978,18.3361745888801,
2.03683249527066));
#194200=CARTESIAN_POINT('Ctrl Pts',(-20.6649460109766,18.3431560104152,
2.03729538221783));
#194201=CARTESIAN_POINT('Ctrl Pts',(-20.6666170559021,18.3468836863881,
2.03754154370137));
#194202=CARTESIAN_POINT('Ctrl Pts',(-20.6711741840977,18.3571288232929,
2.03821543231835));
#194203=CARTESIAN_POINT('Ctrl Pts',(-20.674038188588,18.3636561288024,2.0386418275163));
#194204=CARTESIAN_POINT('Ctrl Pts',(-20.6891489412836,18.3985730439408,
2.04090771294289));
#194205=CARTESIAN_POINT('Ctrl Pts',(-20.7008063082492,18.4272155179464,
2.04271348048651));
#194206=CARTESIAN_POINT('Ctrl Pts',(-20.7341848426354,18.5146675928256,
2.04809769033837));
#194207=CARTESIAN_POINT('Ctrl Pts',(-20.7539266266334,18.5741987773712,
2.05158943073611));
#194208=CARTESIAN_POINT('Ctrl Pts',(-20.824016430556,18.8218628606598,2.06573534679006));
#194209=CARTESIAN_POINT('Ctrl Pts',(-20.850932996752,19.0155969878599,2.07601666321669));
#194210=CARTESIAN_POINT('Ctrl Pts',(-20.8509998750783,19.2102727321581,
2.08722602201617));
#194211=CARTESIAN_POINT('Ctrl Pts',(-20.7227695185423,19.9371792543491,
2.1335156684528));
#194212=CARTESIAN_POINT('Ctrl Pts',(-20.8048848906457,19.7049845745767,
2.11869587197603));
#194213=CARTESIAN_POINT('Ctrl Pts',(-20.8469525718855,19.4574404677657,
2.10387607549926));
#194214=CARTESIAN_POINT('Ctrl Pts',(-20.8478239987731,19.2101685861784,
2.0890562790225));
#194215=CARTESIAN_POINT('Origin',(-18.734,19.211,0.));
#194216=CARTESIAN_POINT('',(-20.7225806782364,19.9371101060755,3.15472451729439));
#194217=CARTESIAN_POINT('',(-20.722580576248,19.9371103853886,2.93545682861291));
#194218=CARTESIAN_POINT('',(-20.7225806064498,19.9371103026755,0.));
#194219=CARTESIAN_POINT('',(-20.850999955063,19.2105638083985,3.11292714750027));
#194220=CARTESIAN_POINT('Ctrl Pts',(-20.7225806782367,19.9371101060747,
3.15472451729435));
#194221=CARTESIAN_POINT('Ctrl Pts',(-20.785411417517,19.7650370374217,3.14472561691515));
#194222=CARTESIAN_POINT('Ctrl Pts',(-20.825700349719,19.5853831201472,3.13494347122732));
#194223=CARTESIAN_POINT('Ctrl Pts',(-20.8447697707137,19.3755532461302,
3.12275001213983));
#194224=CARTESIAN_POINT('Ctrl Pts',(-20.846707234681,19.3484584918627,3.12116300122428));
#194225=CARTESIAN_POINT('Ctrl Pts',(-20.8486554029297,19.31112969335,3.11895645481964));
#194226=CARTESIAN_POINT('Ctrl Pts',(-20.849114096932,19.3009209655022,3.1183509463616));
#194227=CARTESIAN_POINT('Ctrl Pts',(-20.849728275587,19.2846205866491,3.11738069348166));
#194228=CARTESIAN_POINT('Ctrl Pts',(-20.8499314061084,19.2785308103528,
3.11701744584967));
#194229=CARTESIAN_POINT('Ctrl Pts',(-20.8502862993193,19.2663076837636,
3.11628678408661));
#194230=CARTESIAN_POINT('Ctrl Pts',(-20.8504376956161,19.2601743827262,
3.11591936206823));
#194231=CARTESIAN_POINT('Ctrl Pts',(-20.8507174560956,19.2464168823187,
3.11509339266041));
#194232=CARTESIAN_POINT('Ctrl Pts',(-20.850831292037,19.2387925020608,3.11463439433882));
#194233=CARTESIAN_POINT('Ctrl Pts',(-20.8509693632007,19.2242998895109,
3.11375949559301));
#194234=CARTESIAN_POINT('Ctrl Pts',(-20.8510013701658,19.217431828255,3.1133438460819));
#194235=CARTESIAN_POINT('Ctrl Pts',(-20.850999955063,19.2105638083985,3.11292714750027));
#194236=CARTESIAN_POINT('Ctrl Pts',(-20.85099995523,19.2105646193066,3.11292719669993));
#194237=CARTESIAN_POINT('Ctrl Pts',(-20.8509977754103,19.1999654398095,
3.11228412019782));
#194238=CARTESIAN_POINT('Ctrl Pts',(-20.850915995346,19.1893665416074,3.11163855555496));
#194239=CARTESIAN_POINT('Ctrl Pts',(-20.8504276815245,19.1572969635354,
3.10967750172564));
#194240=CARTESIAN_POINT('Ctrl Pts',(-20.8497740575474,19.1358319766212,
3.10835440386201));
#194241=CARTESIAN_POINT('Ctrl Pts',(-20.8411283414657,18.9465942990346,
3.0965948009523));
#194242=CARTESIAN_POINT('Ctrl Pts',(-20.8135227192111,18.7803420861453,
3.08553279276271));
#194243=CARTESIAN_POINT('Ctrl Pts',(-20.7432715722678,18.5390867304095,
3.06893612399543));
#194244=CARTESIAN_POINT('Ctrl Pts',(-20.7152531445003,18.4604818545801,
3.06345029913019));
#194245=CARTESIAN_POINT('Ctrl Pts',(-20.6682556445442,18.3497772264329,
3.05577794756062));
#194246=CARTESIAN_POINT('Ctrl Pts',(-20.6529556395076,18.3162043807657,
3.05345918018755));
#194247=CARTESIAN_POINT('Ctrl Pts',(-20.6334899111243,18.2762895695352,
3.05072678385532));
#194248=CARTESIAN_POINT('Ctrl Pts',(-20.6301587543699,18.2695503234881,
3.05026629891224));
#194249=CARTESIAN_POINT('Ctrl Pts',(-20.6249238390602,18.2591000958969,
3.04955374629547));
#194250=CARTESIAN_POINT('Ctrl Pts',(-20.6230449320338,18.2553768326334,
3.049300171825));
#194251=CARTESIAN_POINT('Ctrl Pts',(-20.6195396037895,18.2484813715494,
3.04883114050058));
#194252=CARTESIAN_POINT('Ctrl Pts',(-20.6179161876382,18.2453077582299,
3.04861550580104));
#194253=CARTESIAN_POINT('Ctrl Pts',(-20.6142273568779,18.2381411740061,
3.04812908442373));
#194254=CARTESIAN_POINT('Ctrl Pts',(-20.6121572409978,18.2341506831601,
3.04785859798749));
#194255=CARTESIAN_POINT('Ctrl Pts',(-20.6060078864863,18.2223885952509,
3.04706231348817));
#194256=CARTESIAN_POINT('Ctrl Pts',(-20.6018929525113,18.2146356285688,
3.04653871361708));
#194257=CARTESIAN_POINT('Ctrl Pts',(-20.5717301719462,18.1586494315956,
3.04276526587493));
#194258=CARTESIAN_POINT('Ctrl Pts',(-20.5438634644742,18.1114140592089,
3.03962253504811));
#194259=CARTESIAN_POINT('Ctrl Pts',(-20.4242378302051,17.9255378147647,
3.02720652788796));
#194260=CARTESIAN_POINT('Ctrl Pts',(-20.3181325530796,17.7968400739698,
3.01845185057355));
#194261=CARTESIAN_POINT('Ctrl Pts',(-20.154583678917,17.6402506638012,3.00591103511555));
#194262=CARTESIAN_POINT('Ctrl Pts',(-20.1093577520868,17.6005026498559,
3.00252978065241));
#194263=CARTESIAN_POINT('Ctrl Pts',(-20.0340386336047,17.5397953261327,
2.99697490314731));
#194264=CARTESIAN_POINT('Ctrl Pts',(-20.0049867810244,17.5175957727333,
2.99484944804649));
#194265=CARTESIAN_POINT('Ctrl Pts',(-19.9687427363683,17.4913586327558,
2.99221161301274));
#194266=CARTESIAN_POINT('Ctrl Pts',(-19.9620817807088,17.4865954088437,
2.9917273929548));
#194267=CARTESIAN_POINT('Ctrl Pts',(-19.9491828825018,17.4774840993406,
2.990790691494));
#194268=CARTESIAN_POINT('Ctrl Pts',(-19.9429488114991,17.4731307343099,
2.99033842102202));
#194269=CARTESIAN_POINT('Ctrl Pts',(-19.9366515568343,17.4687835280316,
2.98988197227961));
#194270=CARTESIAN_POINT('Ctrl Pts',(-19.9366116282065,17.4687559659863,
2.9898790781186));
#194271=CARTESIAN_POINT('Ctrl Pts',(-19.9365301425433,17.4686997219697,
2.9898731717975));
#194272=CARTESIAN_POINT('Ctrl Pts',(-19.9364885854512,17.4686710401278,
2.98987015963466));
#194273=CARTESIAN_POINT('Ctrl Pts',(-19.9364037345947,17.4686124823107,
2.98986400946673));
#194274=CARTESIAN_POINT('Ctrl Pts',(-19.9363604407185,17.4685826064453,
2.98986087145505));
#194275=CARTESIAN_POINT('Ctrl Pts',(-19.936271997837,17.4685215794089,2.98985446100809));
#194276=CARTESIAN_POINT('Ctrl Pts',(-19.9362268486726,17.4684904283363,
2.98985118856294));
#194277=CARTESIAN_POINT('Ctrl Pts',(-19.9361345647791,17.468426761527,2.98984449980009));
#194278=CARTESIAN_POINT('Ctrl Pts',(-19.9360874300691,17.4683942460359,
2.98984108348563));
#194279=CARTESIAN_POINT('Ctrl Pts',(-19.9359910322673,17.4683277525793,
2.98983409663849));
#194280=CARTESIAN_POINT('Ctrl Pts',(-19.9359417689632,17.4682937747276,
2.98983052609251));
#194281=CARTESIAN_POINT('Ctrl Pts',(-19.9358409559903,17.4682242483827,
2.9898232193383));
#194282=CARTESIAN_POINT('Ctrl Pts',(-19.9357894061808,17.4681887000846,
2.98981948312222));
#194283=CARTESIAN_POINT('Ctrl Pts',(-19.9356838453768,17.4681159131875,
2.98981183236436));
#194284=CARTESIAN_POINT('Ctrl Pts',(-19.9356298343095,17.4680786748676,
2.98980791781996));
#194285=CARTESIAN_POINT('Ctrl Pts',(-19.9355191572701,17.4680023753746,
2.98979989637337));
#194286=CARTESIAN_POINT('Ctrl Pts',(-19.9354624911111,17.4679633144452,
2.98979578946063));
#194287=CARTESIAN_POINT('Ctrl Pts',(-19.9353462882075,17.4678832222028,
2.98978736765489));
#194288=CARTESIAN_POINT('Ctrl Pts',(-19.9352867512011,17.4678421911321,
2.9897830527463));
#194289=CARTESIAN_POINT('Ctrl Pts',(-19.9351645654217,17.4677579936901,
2.98977419747979));
#194290=CARTESIAN_POINT('Ctrl Pts',(-19.9351019164488,17.4677148276627,
2.98976965711124));
#194291=CARTESIAN_POINT('Ctrl Pts',(-19.9349732364898,17.4676261755824,
2.98976033135096));
#194292=CARTESIAN_POINT('Ctrl Pts',(-19.9349072052411,17.4675806899001,
2.98975554594462));
#194293=CARTESIAN_POINT('Ctrl Pts',(-19.9347714564812,17.4674871906218,
2.98974570807275));
#194294=CARTESIAN_POINT('Ctrl Pts',(-19.9347017386606,17.4674391774465,
2.98974065558987));
#194295=CARTESIAN_POINT('Ctrl Pts',(-19.9345582726968,17.4673403881846,
2.98973025864625));
#194296=CARTESIAN_POINT('Ctrl Pts',(-19.9344845242288,17.4672896126064,
2.98972491416782));
#194297=CARTESIAN_POINT('Ctrl Pts',(-19.9343326063573,17.4671850318566,
2.9897139049437));
#194298=CARTESIAN_POINT('Ctrl Pts',(-19.9342544365194,17.4671312272361,
2.98970824017331));
#194299=CARTESIAN_POINT('Ctrl Pts',(-19.9340932297034,17.4670202838966,
2.98969655805073));
#194300=CARTESIAN_POINT('Ctrl Pts',(-19.9340101923363,17.4669631459029,
2.98969054067828));
#194301=CARTESIAN_POINT('Ctrl Pts',(-19.9338387387249,17.4668451867533,
2.98967811629242));
#194302=CARTESIAN_POINT('Ctrl Pts',(-19.9337503218969,17.4667843663627,
2.98967170924602));
#194303=CARTESIAN_POINT('Ctrl Pts',(-19.9335675181791,17.4666586393566,
2.98965846270114));
#194304=CARTESIAN_POINT('Ctrl Pts',(-19.9334731306912,17.4665937337101,
2.98965162317032));
#194305=CARTESIAN_POINT('Ctrl Pts',(-19.9332776976403,17.4664593673469,
2.98963746183536));
#194306=CARTESIAN_POINT('Ctrl Pts',(-19.9331766513016,17.4663899077427,
2.98963013998798));
#194307=CARTESIAN_POINT('Ctrl Pts',(-19.9329671029273,17.4662458902671,
2.98961495626448));
#194308=CARTESIAN_POINT('Ctrl Pts',(-19.9328585963718,17.4661713312655,
2.98960709407647));
#194309=CARTESIAN_POINT('Ctrl Pts',(-19.9326331730472,17.4660164652386,
2.98959076055715));
#194310=CARTESIAN_POINT('Ctrl Pts',(-19.9325162562616,17.4659361605959,
2.98958228924378));
#194311=CARTESIAN_POINT('Ctrl Pts',(-19.9272497752479,17.4623196413682,
2.98920070767884));
#194312=CARTESIAN_POINT('Ctrl Pts',(-19.9220846377868,17.4588062564452,
2.98882673450909));
#194313=CARTESIAN_POINT('Ctrl Pts',(-19.9101877430885,17.4507906433636,
2.98796592842409));
#194314=CARTESIAN_POINT('Ctrl Pts',(-19.903445581029,17.4463041008862,2.9874785105995));
#194315=CARTESIAN_POINT('Ctrl Pts',(-19.8836695874574,17.4333073543324,
2.9860499362193));
#194316=CARTESIAN_POINT('Ctrl Pts',(-19.8705676486739,17.4249022248315,
2.98510487651262));
#194317=CARTESIAN_POINT('Ctrl Pts',(-19.758331169233,17.3546355149255,2.9770193353589));
#194318=CARTESIAN_POINT('Ctrl Pts',(-19.6543404957147,17.3009452859684,
2.96957791062179));
#194319=CARTESIAN_POINT('Ctrl Pts',(-19.3961388602265,17.1936345862814,
2.95131355151301));
#194320=CARTESIAN_POINT('Ctrl Pts',(-19.2391098901707,17.148706333767,2.94035030369415));
#194321=CARTESIAN_POINT('Ctrl Pts',(-19.0464926728137,17.1169396705471,
2.92794662346129));
#194322=CARTESIAN_POINT('Ctrl Pts',(-19.0143814710994,17.1123988394046,
2.92591453207428));
#194323=CARTESIAN_POINT('Ctrl Pts',(-18.9749926611102,17.1077492145261,
2.92347561768575));
#194324=CARTESIAN_POINT('Ctrl Pts',(-18.9678042213774,17.1069379954831,
2.92303269851357));
#194325=CARTESIAN_POINT('Ctrl Pts',(-18.9565268377359,17.1057238457736,
2.92234140580566));
#194326=CARTESIAN_POINT('Ctrl Pts',(-18.9524407174705,17.1052959532069,
2.92209166429393));
#194327=CARTESIAN_POINT('Ctrl Pts',(-18.9447996294934,17.1045182707032,
2.92162604928551));
#194328=CARTESIAN_POINT('Ctrl Pts',(-18.9412450614059,17.104165586856,2.92141002079775));
#194329=CARTESIAN_POINT('Ctrl Pts',(-18.9331275660419,17.1033809123853,
2.92091796865442));
#194330=CARTESIAN_POINT('Ctrl Pts',(-18.9285641266738,17.1029547425271,
2.92064227481427));
#194331=CARTESIAN_POINT('Ctrl Pts',(-18.914528527399,17.1016899529705,2.9197970777449));
#194332=CARTESIAN_POINT('Ctrl Pts',(-18.9050519220118,17.1009003172099,
2.91923025507764));
#194333=CARTESIAN_POINT('Ctrl Pts',(-18.7766113584994,17.0910690177648,
2.91159598309741));
#194334=CARTESIAN_POINT('Ctrl Pts',(-18.6570773640448,17.092034620886,2.90504371645033));
#194335=CARTESIAN_POINT('Ctrl Pts',(-18.4296594082806,17.1131537684383,
2.8926109792909));
#194336=CARTESIAN_POINT('Ctrl Pts',(-18.3220142797846,17.1316133462094,
2.8867373085778));
#194337=CARTESIAN_POINT('Ctrl Pts',(-18.143322514997,17.1766820108722,2.87648730374147));
#194338=CARTESIAN_POINT('Ctrl Pts',(-18.0714096980329,17.1989557787946,
2.87222125854008));
#194339=CARTESIAN_POINT('Ctrl Pts',(-17.9831708519841,17.2315305461036,
2.8667293547082));
#194340=CARTESIAN_POINT('Ctrl Pts',(-17.9655904226102,17.2382885624412,
2.86562218317031));
#194341=CARTESIAN_POINT('Ctrl Pts',(-17.9401553053867,17.2484575516588,
2.86400042499205));
#194342=CARTESIAN_POINT('Ctrl Pts',(-17.9322271334331,17.2516831476604,
2.86349207839713));
#194343=CARTESIAN_POINT('Ctrl Pts',(-17.9183591816658,17.2574236235625,
2.86259779381244));
#194344=CARTESIAN_POINT('Ctrl Pts',(-17.9124108923423,17.2599177516402,
2.86221256336359));
#194345=CARTESIAN_POINT('Ctrl Pts',(-17.9008813289732,17.2648141915301,
2.86146262116881));
#194346=CARTESIAN_POINT('Ctrl Pts',(-17.895298811504,17.2672134282999,2.86109801723052));
#194347=CARTESIAN_POINT('Ctrl Pts',(-17.8819756874295,17.2730074788069,
2.8602242601708));
#194348=CARTESIAN_POINT('Ctrl Pts',(-17.874244976147,17.2764246623278,2.85971434508585));
#194349=CARTESIAN_POINT('Ctrl Pts',(-17.8464078225822,17.2889292482502,
2.85786751990641));
#194350=CARTESIAN_POINT('Ctrl Pts',(-17.8264238299025,17.2982843165305,
2.85652144180748));
#194351=CARTESIAN_POINT('Ctrl Pts',(-17.6393416843702,17.3894546890769,
2.84372334794477));
#194352=CARTESIAN_POINT('Ctrl Pts',(-17.4835971715653,17.4926376674441,
2.83146747950523));
#194353=CARTESIAN_POINT('Ctrl Pts',(-17.2831655959475,17.6672562575808,
2.81391777144383));
#194354=CARTESIAN_POINT('Ctrl Pts',(-17.2259703466318,17.7230774609551,
2.80867204112289));
#194355=CARTESIAN_POINT('Ctrl Pts',(-17.1477960780451,17.8085241501172,
2.80129000096494));
#194356=CARTESIAN_POINT('Ctrl Pts',(-17.1242073511821,17.8356639045859,
2.7990314943008));
#194357=CARTESIAN_POINT('Ctrl Pts',(-17.0965701300872,17.8691475140997,
2.79636045805782));
#194358=CARTESIAN_POINT('Ctrl Pts',(-17.0918508289035,17.8749271066005,
2.79590344222051));
#194359=CARTESIAN_POINT('Ctrl Pts',(-17.084549169472,17.8839663724423,2.79519508429811));
#194360=CARTESIAN_POINT('Ctrl Pts',(-17.0819457457191,17.8872088410185,
2.79494226328094));
#194361=CARTESIAN_POINT('Ctrl Pts',(-17.0771274978094,17.8932461430462,
2.79447391830848));
#194362=CARTESIAN_POINT('Ctrl Pts',(-17.0749102024703,17.896038875084,2.79425822096408));
#194363=CARTESIAN_POINT('Ctrl Pts',(-17.0699034054958,17.9023778694491,
2.79377076000355));
#194364=CARTESIAN_POINT('Ctrl Pts',(-17.0671181849839,17.9059274456788,
2.793499302157));
#194365=CARTESIAN_POINT('Ctrl Pts',(-17.0589012460277,17.9164685987238,
2.79269749824917));
#194366=CARTESIAN_POINT('Ctrl Pts',(-17.0535019373629,17.9234854749911,
2.79216939607174));
#194367=CARTESIAN_POINT('Ctrl Pts',(-17.0137761000571,17.9757883448498,
2.78827284917072));
#194368=CARTESIAN_POINT('Ctrl Pts',(-16.9812381365477,18.0224104331941,
2.7850195988906));
#194369=CARTESIAN_POINT('Ctrl Pts',(-16.9357152036213,18.0935809974637,
2.78028178135635));
#194370=CARTESIAN_POINT('Ctrl Pts',(-16.9212746062238,18.1171626424178,
2.77874739362743));
#194371=CARTESIAN_POINT('Ctrl Pts',(-16.8895811214755,18.1712707107043,
2.77529118226473));
#194372=CARTESIAN_POINT('Ctrl Pts',(-16.8726163054525,18.2019564782933,
2.77337620346514));
#194373=CARTESIAN_POINT('Ctrl Pts',(-16.805948584421,18.3299526913423,2.76551935850843));
#194374=CARTESIAN_POINT('Ctrl Pts',(-16.7630542108576,18.4306164895672,
2.75963568995538));
#194375=CARTESIAN_POINT('Ctrl Pts',(-16.7105369056274,18.586251065365,2.75050163253197));
#194376=CARTESIAN_POINT('Ctrl Pts',(-16.6949902021556,18.6390275113436,
2.74740000704839));
#194377=CARTESIAN_POINT('Ctrl Pts',(-16.6731235544017,18.725561115507,2.74226487875214));
#194378=CARTESIAN_POINT('Ctrl Pts',(-16.6655382976033,18.7589727612832,
2.74027058544756));
#194379=CARTESIAN_POINT('Ctrl Pts',(-16.6566319574282,18.8031425176688,
2.73761316136558));
#194380=CARTESIAN_POINT('Ctrl Pts',(-16.6545777056313,18.8137486622724,
2.73697348621668));
#194381=CARTESIAN_POINT('Ctrl Pts',(-16.6513451572067,18.8311508543501,
2.73592118537163));
#194382=CARTESIAN_POINT('Ctrl Pts',(-16.6501187192852,18.8379378418858,
2.73551009862636));
#194383=CARTESIAN_POINT('Ctrl Pts',(-16.6478082738142,18.8510905964199,
2.73471207155915));
#194384=CARTESIAN_POINT('Ctrl Pts',(-16.6467201827165,18.8574555754656,
2.73432526608893));
#194385=CARTESIAN_POINT('Ctrl Pts',(-16.6442742142628,18.872168663406,2.73342966864509));
#194386=CARTESIAN_POINT('Ctrl Pts',(-16.6429372177709,18.8805200887094,
2.73292021953313));
#194387=CARTESIAN_POINT('Ctrl Pts',(-16.6394743591176,18.9030132384448,
2.73154507240444));
#194388=CARTESIAN_POINT('Ctrl Pts',(-16.6374417152992,18.9171686730325,
2.73067644075851));
#194389=CARTESIAN_POINT('Ctrl Pts',(-16.6200061350573,19.0479992694939,
2.72261719298556));
#194390=CARTESIAN_POINT('Ctrl Pts',(-16.6142165511034,19.165729025055,2.71512023312754));
#194391=CARTESIAN_POINT('Ctrl Pts',(-16.6238232368497,19.4468024093604,
2.69674435040332));
#194392=CARTESIAN_POINT('Ctrl Pts',(-16.6483407182322,19.6090885168231,
2.68572645352123));
#194393=CARTESIAN_POINT('Ctrl Pts',(-16.6994365607521,19.7968335156138,
2.67338067920544));
#194394=CARTESIAN_POINT('Ctrl Pts',(-16.7082303693405,19.8265541686603,
2.67144052449234));
#194395=CARTESIAN_POINT('Ctrl Pts',(-16.7198475785932,19.8628664755711,
2.6690966282912));
#194396=CARTESIAN_POINT('Ctrl Pts',(-16.7220554157931,19.8696492784876,
2.66865996345441));
#194397=CARTESIAN_POINT('Ctrl Pts',(-16.7255819053651,19.8802999730684,
2.66797625184641));
#194398=CARTESIAN_POINT('Ctrl Pts',(-16.726877522471,19.8841753543147,2.66772788516232));
#194399=CARTESIAN_POINT('Ctrl Pts',(-16.7293278647538,19.891434724609,2.66726344615056));
#194400=CARTESIAN_POINT('Ctrl Pts',(-16.7304799288485,19.894819500299,2.66704722715218));
#194401=CARTESIAN_POINT('Ctrl Pts',(-16.7331395357272,19.9025690315533,
2.66655293051639));
#194402=CARTESIAN_POINT('Ctrl Pts',(-16.7346527851077,19.9069317769167,
2.66627519426601));
#194403=CARTESIAN_POINT('Ctrl Pts',(-16.7393842309852,19.920429872482,2.6654174585691));
#194404=CARTESIAN_POINT('Ctrl Pts',(-16.7426509064998,19.9295482627064,
2.66484025636619));
#194405=CARTESIAN_POINT('Ctrl Pts',(-16.7824124744682,20.0381821222546,
2.65798667197639));
#194406=CARTESIAN_POINT('Ctrl Pts',(-16.826274378671,20.1348577946083,2.65211547231414));
#194407=CARTESIAN_POINT('Ctrl Pts',(-16.88333536993,20.239052788475,2.64562755017659));
#194408=CARTESIAN_POINT('Ctrl Pts',(-16.8895710858579,20.2501987743916,
2.64493143250745));
#194409=CARTESIAN_POINT('Ctrl Pts',(-16.9500544790224,20.3560498500362,
2.63829480520645));
#194410=CARTESIAN_POINT('Ctrl Pts',(-17.0114482111197,20.4464817715604,
2.63241692555868));
#194411=CARTESIAN_POINT('Ctrl Pts',(-17.126560946372,20.5906773261895,2.62215551166551));
#194412=CARTESIAN_POINT('Ctrl Pts',(-17.1766920750684,20.6470223322504,
2.61788215953077));
#194413=CARTESIAN_POINT('Ctrl Pts',(-17.2429820636454,20.7139670412145,
2.61238144921584));
#194414=CARTESIAN_POINT('Ctrl Pts',(-17.2564250843209,20.727184932008,2.61127322406143));
#194415=CARTESIAN_POINT('Ctrl Pts',(-17.2762277387244,20.7461424533672,
2.60965020281947));
#194416=CARTESIAN_POINT('Ctrl Pts',(-17.2824487445255,20.7520260436863,
2.60914166067777));
#194417=CARTESIAN_POINT('Ctrl Pts',(-17.293418569446,20.7622755241157,2.60824715007469));
#194418=CARTESIAN_POINT('Ctrl Pts',(-17.2981519975476,20.7666577779864,
2.60786189027519));
#194419=CARTESIAN_POINT('Ctrl Pts',(-17.3073822266992,20.7751251989829,
2.60711197864455));
#194420=CARTESIAN_POINT('Ctrl Pts',(-17.3118767345711,20.7792127808178,
2.6067474350332));
#194421=CARTESIAN_POINT('Ctrl Pts',(-17.3226634440892,20.7889383715966,
2.60587396433251));
#194422=CARTESIAN_POINT('Ctrl Pts',(-17.3289718873195,20.7945581384804,
2.60536427640623));
#194423=CARTESIAN_POINT('Ctrl Pts',(-17.3518589644793,20.8147022680002,
2.60351911870323));
#194424=CARTESIAN_POINT('Ctrl Pts',(-17.3686300963038,20.8290048748068,
2.60217450247361));
#194425=CARTESIAN_POINT('Ctrl Pts',(-17.5292434351453,20.961702178104,2.58936291310832));
#194426=CARTESIAN_POINT('Ctrl Pts',(-17.6878756334158,21.0608628026699,
2.57708963256288));
#194427=CARTESIAN_POINT('Ctrl Pts',(-17.9299184228805,21.1709723982243,
2.55953486186786));
#194428=CARTESIAN_POINT('Ctrl Pts',(-18.0042627360628,21.1998499722629,
2.55430033562526));
#194429=CARTESIAN_POINT('Ctrl Pts',(-18.1142120499929,21.2355594814582,
2.54693189779709));
#194430=CARTESIAN_POINT('Ctrl Pts',(-18.1486405530848,21.2457807915411,
2.54467625192697));
#194431=CARTESIAN_POINT('Ctrl Pts',(-18.1905166143594,21.2570621794086,
2.54200813289057));
#194432=CARTESIAN_POINT('Ctrl Pts',(-18.1977288921983,21.2589643393422,
2.5415512845431));
#194433=CARTESIAN_POINT('Ctrl Pts',(-18.2089769290744,21.2618673923712,
2.54084312920023));
#194434=CARTESIAN_POINT('Ctrl Pts',(-18.2130057554708,21.2628945596569,
2.54059034461245));
#194435=CARTESIAN_POINT('Ctrl Pts',(-18.2204956783852,21.2647806669998,
2.54012203267311));
#194436=CARTESIAN_POINT('Ctrl Pts',(-18.2239558860916,21.26564272286,2.53990633214794));
#194437=CARTESIAN_POINT('Ctrl Pts',(-18.2317998435727,21.2675758839695,
2.53941882020694));
#194438=CARTESIAN_POINT('Ctrl Pts',(-18.2361848385281,21.2686417155364,
2.53914731483113));
#194439=CARTESIAN_POINT('Ctrl Pts',(-18.2475193459509,21.2713583652125,
2.53844809037181));
#194440=CARTESIAN_POINT('Ctrl Pts',(-18.2544739301075,21.2729880628731,
2.53802155703353));
#194441=CARTESIAN_POINT('Ctrl Pts',(-18.2973116080084,21.2827979503608,
2.53540885043659));
#194442=CARTESIAN_POINT('Ctrl Pts',(-18.3333970779269,21.2900769983733,
2.53327078911107));
#194443=CARTESIAN_POINT('Ctrl Pts',(-18.5372529005305,21.3256927790929,
2.52145104972034));
#194444=CARTESIAN_POINT('Ctrl Pts',(-18.7077826973774,21.334666545312,2.5124978338181));
#194445=CARTESIAN_POINT('Ctrl Pts',(-18.9729231896225,21.3166449397461,
2.49788064924861));
#194446=CARTESIAN_POINT('Ctrl Pts',(-19.0677262227037,21.3037132206297,
2.49252200499758));
#194447=CARTESIAN_POINT('Ctrl Pts',(-19.18229797623,21.2801004038947,2.48571044509213));
#194448=CARTESIAN_POINT('Ctrl Pts',(-19.2032037384758,21.2754600648055,
2.48445395424378));
#194449=CARTESIAN_POINT('Ctrl Pts',(-19.2328037468124,21.2684170862731,
2.48265414763837));
#194450=CARTESIAN_POINT('Ctrl Pts',(-19.2415590085599,21.266274700308,2.4821191940547));
#194451=CARTESIAN_POINT('Ctrl Pts',(-19.2566302414693,21.2624846413908,
2.48119374149794));
#194452=CARTESIAN_POINT('Ctrl Pts',(-19.2629528116407,21.2608635380793,
2.48080410506403));
#194453=CARTESIAN_POINT('Ctrl Pts',(-19.275038000158,21.2577052675881,2.48005662277461));
#194454=CARTESIAN_POINT('Ctrl Pts',(-19.2808018258988,21.2561729345095,
2.47969893689682));
#194455=CARTESIAN_POINT('Ctrl Pts',(-19.2957593893355,21.2521286639712,
2.47876759098365));
#194456=CARTESIAN_POINT('Ctrl Pts',(-19.304942700576,21.2495789811543,2.47819270922806));
#194457=CARTESIAN_POINT('Ctrl Pts',(-19.3361290817075,21.2406930429304,
2.47622976620224));
#194458=CARTESIAN_POINT('Ctrl Pts',(-19.3580458404042,21.2340620366225,
2.47483214555194));
#194459=CARTESIAN_POINT('Ctrl Pts',(-19.5482025801118,21.1731453441004,
2.46254288034587));
#194460=CARTESIAN_POINT('Ctrl Pts',(-19.7091066967145,21.0983481876638,
2.45093578208277));
#194461=CARTESIAN_POINT('Ctrl Pts',(-19.9317626182106,20.95870387719,2.43357188735246));
#194462=CARTESIAN_POINT('Ctrl Pts',(-20.0018586109472,20.9085395630027,
2.42789886920743));
#194463=CARTESIAN_POINT('Ctrl Pts',(-20.097888640167,20.8305400845952,2.42000168768567));
#194464=CARTESIAN_POINT('Ctrl Pts',(-20.126435187597,20.8060633090678,2.41763728485151));
#194465=CARTESIAN_POINT('Ctrl Pts',(-20.159921574675,20.7757663709232,2.414858530903));
#194466=CARTESIAN_POINT('Ctrl Pts',(-20.1654994803408,20.7706651481769,
2.41439549131404));
#194467=CARTESIAN_POINT('Ctrl Pts',(-20.1741190148305,20.7626970356697,
2.41367985103559));
#194468=CARTESIAN_POINT('Ctrl Pts',(-20.1771796121016,20.7598508886571,
2.41342572288789));
#194469=CARTESIAN_POINT('Ctrl Pts',(-20.1828344744696,20.754560937399,2.41295618287214));
#194470=CARTESIAN_POINT('Ctrl Pts',(-20.185430974356,20.7521196672717,2.41274058989437));
#194471=CARTESIAN_POINT('Ctrl Pts',(-20.1912801487014,20.7465922868005,
2.41225491288289));
#194472=CARTESIAN_POINT('Ctrl Pts',(-20.1945291821626,20.7435024019499,
2.41198512511031));
#194473=CARTESIAN_POINT('Ctrl Pts',(-20.2040697009577,20.7343713112875,
2.41119279953939));
#194474=CARTESIAN_POINT('Ctrl Pts',(-20.2103337839112,20.7283014341696,
2.41067242744472));
#194475=CARTESIAN_POINT('Ctrl Pts',(-20.2546652361281,20.684809930901,2.40698706660287));
#194476=CARTESIAN_POINT('Ctrl Pts',(-20.2913461219772,20.6459956622131,
2.40392359083267));
#194477=CARTESIAN_POINT('Ctrl Pts',(-20.3355350676358,20.5955437882601,
2.40015196205096));
#194478=CARTESIAN_POINT('Ctrl Pts',(-20.3444470216982,20.5851675575748,
2.39938689808646));
#194479=CARTESIAN_POINT('Ctrl Pts',(-20.3868880904001,20.5347732200816,
2.39571808119312));
#194480=CARTESIAN_POINT('Ctrl Pts',(-20.4190308258731,20.4936090895913,
2.3928615197817));
#194481=CARTESIAN_POINT('Ctrl Pts',(-20.5137301795037,20.3626178607048,
2.38406090155473));
#194482=CARTESIAN_POINT('Ctrl Pts',(-20.5708676911869,20.2691018000445,
2.37816904471015));
#194483=CARTESIAN_POINT('Ctrl Pts',(-20.6549212208048,20.1040280606797,
2.36786973125037));
#194484=CARTESIAN_POINT('Ctrl Pts',(-20.6856664530823,20.0346709047926,
2.36357209760958));
#194485=CARTESIAN_POINT('Ctrl Pts',(-20.7160027946319,19.954938307128,2.35859155954439));
#194486=CARTESIAN_POINT('Ctrl Pts',(-20.719321761882,19.9460352209481,2.35803492211194));
#194487=CARTESIAN_POINT('Ctrl Pts',(-20.7225806064941,19.9371103025544,
2.35747633162257));
#194488=CARTESIAN_POINT('',(-20.8499621049652,19.2128841874121,2.8890562790225));
#194489=CARTESIAN_POINT('Ctrl Pts',(-20.8499621049652,19.2128841874121,
2.8890562790225));
#194490=CARTESIAN_POINT('Ctrl Pts',(-20.845633252063,18.7070050108363,2.85866010167885));
#194491=CARTESIAN_POINT('Ctrl Pts',(-20.4101935901701,17.4889118801332,
2.78587198877473));
#194492=CARTESIAN_POINT('Ctrl Pts',(-18.3741968228298,16.7337288824509,
2.6706919403101));
#194493=CARTESIAN_POINT('Ctrl Pts',(-16.4562523864159,18.1726376448454,
2.54351613362869));
#194494=CARTESIAN_POINT('Ctrl Pts',(-16.6280000106062,20.564179464316,2.41634032694724));
#194495=CARTESIAN_POINT('Ctrl Pts',(-18.731871915622,21.7142630277803,2.28916452026582));
#194496=CARTESIAN_POINT('Ctrl Pts',(-20.2929105264368,20.8643639334257,
2.194889634101));
#194497=CARTESIAN_POINT('Ctrl Pts',(-20.6701805215755,20.085883266734,2.14300668349666));
#194498=CARTESIAN_POINT('Ctrl Pts',(-20.7227695185423,19.9371792543491,
2.1335156684528));
#194499=CARTESIAN_POINT('Ctrl Pts',(-20.8509991255307,19.2129241887627,
2.88845980109392));
#194500=CARTESIAN_POINT('Ctrl Pts',(-20.850855388126,19.3710645780658,2.8988202813796));
#194501=CARTESIAN_POINT('Ctrl Pts',(-20.832993119571,19.5286963706424,2.90945375295789));
#194502=CARTESIAN_POINT('Ctrl Pts',(-20.7934894773314,19.7014647873359,
2.92067365423454));
#194503=CARTESIAN_POINT('Ctrl Pts',(-20.7889879759962,19.7199961557791,
2.92187071866517));
#194504=CARTESIAN_POINT('Ctrl Pts',(-20.7809486400232,19.7512447612192,
2.92387556393314));
#194505=CARTESIAN_POINT('Ctrl Pts',(-20.7775412260559,19.763994045634,2.92468963664369));
#194506=CARTESIAN_POINT('Ctrl Pts',(-20.7726159275808,19.7817552018483,
2.92581747267831));
#194507=CARTESIAN_POINT('Ctrl Pts',(-20.7711984117392,19.7867942628903,
2.92613674703618));
#194508=CARTESIAN_POINT('Ctrl Pts',(-20.7687546217206,19.7953595777528,
2.92667817863929));
#194509=CARTESIAN_POINT('Ctrl Pts',(-20.7677378406046,19.7988884954982,
2.92690088220672));
#194510=CARTESIAN_POINT('Ctrl Pts',(-20.7657731499416,19.8056412010862,
2.92732630744239));
#194511=CARTESIAN_POINT('Ctrl Pts',(-20.7648267450337,19.8088653885898,
2.92752911793041));
#194512=CARTESIAN_POINT('Ctrl Pts',(-20.7623032579457,19.8173872075475,
2.92806436237892));
#194513=CARTESIAN_POINT('Ctrl Pts',(-20.7607130854098,19.8226809811204,
2.92839603643779));
#194514=CARTESIAN_POINT('Ctrl Pts',(-20.7550185535674,19.841372386282,2.92956441330896));
#194515=CARTESIAN_POINT('Ctrl Pts',(-20.7508018310205,19.854735766525,2.93039481478052));
#194516=CARTESIAN_POINT('Ctrl Pts',(-20.7388900140446,19.8912196309275,
2.93265089211074));
#194517=CARTESIAN_POINT('Ctrl Pts',(-20.7309311654813,19.9142408329297,
2.93406225781276));
#194518=CARTESIAN_POINT('Ctrl Pts',(-20.722580576248,19.9371103853886,2.93545682861291));
#194519=CARTESIAN_POINT('Origin',(-18.734,19.211,0.));
#194520=CARTESIAN_POINT('',(-20.7225806759744,19.9371101122702,3.95421657486109));
#194521=CARTESIAN_POINT('',(-20.7225806064494,19.9371103026767,3.73234504707874));
#194522=CARTESIAN_POINT('',(-20.7225806064498,19.9371103026755,0.));
#194523=CARTESIAN_POINT('Ctrl Pts',(-20.7225806759744,19.9371101122702,
3.95421657486109));
#194524=CARTESIAN_POINT('Ctrl Pts',(-20.7432514903791,19.8804994393335,
3.95029631842219));
#194525=CARTESIAN_POINT('Ctrl Pts',(-20.7615069746506,19.8230005145436,
3.94643459043925));
#194526=CARTESIAN_POINT('Ctrl Pts',(-20.7804090216855,19.7532558144153,
3.94195341122591));
#194527=CARTESIAN_POINT('Ctrl Pts',(-20.7834316339718,19.7417176697722,
3.94121863712442));
#194528=CARTESIAN_POINT('Ctrl Pts',(-20.7875891289675,19.725281973163,3.94018189259722));
#194529=CARTESIAN_POINT('Ctrl Pts',(-20.788804268635,19.7204052191809,3.9398755087063));
#194530=CARTESIAN_POINT('Ctrl Pts',(-20.7908681039204,19.7119948194786,
3.93934930571094));
#194531=CARTESIAN_POINT('Ctrl Pts',(-20.7917250850485,19.7084632460899,
3.93912901274259));
#194532=CARTESIAN_POINT('Ctrl Pts',(-20.7933688049833,19.7016126368667,
3.93870298798722));
#194533=CARTESIAN_POINT('Ctrl Pts',(-20.7941566161855,19.6982939067538,
3.9384971923441));
#194534=CARTESIAN_POINT('Ctrl Pts',(-20.796259960111,19.6893370935663,3.93794332966228));
#194535=CARTESIAN_POINT('Ctrl Pts',(-20.7975604025928,19.6836954461399,
3.93759612417221));
#194536=CARTESIAN_POINT('Ctrl Pts',(-20.8022980768524,19.66275002125,3.93631297583456));
#194537=CARTESIAN_POINT('Ctrl Pts',(-20.8055884394275,19.6474130916265,
3.93538507921685));
#194538=CARTESIAN_POINT('Ctrl Pts',(-20.8354454541131,19.5002904502564,
3.9265831659023));
#194539=CARTESIAN_POINT('Ctrl Pts',(-20.8495760163056,19.3662740352944,
3.91931203515023));
#194540=CARTESIAN_POINT('Ctrl Pts',(-20.8509595375063,19.2255206442362,
3.91166810814775));
#194541=CARTESIAN_POINT('Ctrl Pts',(-20.8509933270378,19.2192332133599,
3.91132667341362));
#194542=CARTESIAN_POINT('Ctrl Pts',(-20.8511331455132,19.0671072341399,
3.90306444324088));
#194543=CARTESIAN_POINT('Ctrl Pts',(-20.8361978950863,18.9216640281003,
3.89510372735859));
#194544=CARTESIAN_POINT('Ctrl Pts',(-20.8015323055344,18.7553942923716,
3.8852444687199));
#194545=CARTESIAN_POINT('Ctrl Pts',(-20.7962279556996,18.7319570117017,
3.88383768620377));
#194546=CARTESIAN_POINT('Ctrl Pts',(-20.7882195562543,18.6991743711183,
3.88184395681023));
#194547=CARTESIAN_POINT('Ctrl Pts',(-20.7858481761669,18.6897490845538,
3.88126770468889));
#194548=CARTESIAN_POINT('Ctrl Pts',(-20.781908381504,18.6745335580391,3.8803323966953));
#194549=CARTESIAN_POINT('Ctrl Pts',(-20.7803800924634,18.6687330008068,
3.87997464207438));
#194550=CARTESIAN_POINT('Ctrl Pts',(-20.7771446742841,18.6566615857626,
3.87922760908645));
#194551=CARTESIAN_POINT('Ctrl Pts',(-20.7754332819468,18.6503919448913,
3.87883819566093));
#194552=CARTESIAN_POINT('Ctrl Pts',(-20.7713216375678,18.6355975519863,
3.87791589776476));
#194553=CARTESIAN_POINT('Ctrl Pts',(-20.7688967218961,18.6270798345886,
3.87738221533758));
#194554=CARTESIAN_POINT('Ctrl Pts',(-20.7606830626322,18.5989013000478,
3.87560764047356));
#194555=CARTESIAN_POINT('Ctrl Pts',(-20.7546623949245,18.5793098115203,
3.87435920727821));
#194556=CARTESIAN_POINT('Ctrl Pts',(-20.7212770023923,18.4760372207133,
3.86769851033935));
#194557=CARTESIAN_POINT('Ctrl Pts',(-20.6889996910731,18.3940465179559,
3.86212559133135));
#194558=CARTESIAN_POINT('Ctrl Pts',(-20.5968951046246,18.1970657457696,
3.84804782489255));
#194559=CARTESIAN_POINT('Ctrl Pts',(-20.5314380705507,18.0850987712143,
3.8394138991219));
#194560=CARTESIAN_POINT('Ctrl Pts',(-20.4404261756852,17.9577913240164,
3.82914906247664));
#194561=CARTESIAN_POINT('Ctrl Pts',(-20.4242561905604,17.9360661334745,
3.82738107538567));
#194562=CARTESIAN_POINT('Ctrl Pts',(-20.3724974459434,17.8692418342402,
3.82190424442907));
#194563=CARTESIAN_POINT('Ctrl Pts',(-20.3354839864957,17.8252730584197,
3.81824361855776));
#194564=CARTESIAN_POINT('Ctrl Pts',(-20.2907363631564,17.7763085059287,
3.81415058119492));
#194565=CARTESIAN_POINT('Ctrl Pts',(-20.2847071386254,17.7697938509429,
3.81360566751355));
#194566=CARTESIAN_POINT('Ctrl Pts',(-20.2755483343229,17.7600216634201,
3.81278802704059));
#194567=CARTESIAN_POINT('Ctrl Pts',(-20.2724490988911,17.7567360035834,
3.81251307176792));
#194568=CARTESIAN_POINT('Ctrl Pts',(-20.2668839722237,17.7508738252702,
3.81202246825166));
#194569=CARTESIAN_POINT('Ctrl Pts',(-20.2644220727579,17.7482936049031,
3.81180652034107));
#194570=CARTESIAN_POINT('Ctrl Pts',(-20.2590779441154,17.7427208964985,
3.81134010380499));
#194571=CARTESIAN_POINT('Ctrl Pts',(-20.256193431545,17.7397306775953,3.81108981710817));
#194572=CARTESIAN_POINT('Ctrl Pts',(-20.2481154338852,17.7314058386046,
3.81039290268273));
#194573=CARTESIAN_POINT('Ctrl Pts',(-20.2429025240412,17.7260900342973,
3.80994776240585));
#194574=CARTESIAN_POINT('Ctrl Pts',(-20.2125439966636,17.6954572297961,
3.80738106408755));
#194575=CARTESIAN_POINT('Ctrl Pts',(-20.1867879389767,17.6707500910073,
3.8053047276702));
#194576=CARTESIAN_POINT('Ctrl Pts',(-20.1021428189004,17.5935656325941,
3.79874985702829));
#194577=CARTESIAN_POINT('Ctrl Pts',(-20.0409390952215,17.5437205258226,
3.79440839539127));
#194578=CARTESIAN_POINT('Ctrl Pts',(-19.9033622252448,17.4439182753741,
3.78513898159681));
#194579=CARTESIAN_POINT('Ctrl Pts',(-19.8262581557949,17.3952473096775,
3.78023202309352));
#194580=CARTESIAN_POINT('Ctrl Pts',(-19.6529388749741,17.3008873441964,
3.76938626865495));
#194581=CARTESIAN_POINT('Ctrl Pts',(-19.555937582257,17.2571849194045,3.76342359210836));
#194582=CARTESIAN_POINT('Ctrl Pts',(-19.4428144227744,17.2161390854988,
3.75637198242424));
#194583=CARTESIAN_POINT('Ctrl Pts',(-19.4295076493934,17.2114607907256,
3.75554120807912));
#194584=CARTESIAN_POINT('Ctrl Pts',(-19.4082024232918,17.2042088624856,
3.75420860148586));
#194585=CARTESIAN_POINT('Ctrl Pts',(-19.4002335378382,17.2015492175387,
3.7537096145858));
#194586=CARTESIAN_POINT('Ctrl Pts',(-19.3861206020294,17.1969321513491,
3.75282485681574));
#194587=CARTESIAN_POINT('Ctrl Pts',(-19.3799830095107,17.1949552265478,
3.75243973437528));
#194588=CARTESIAN_POINT('Ctrl Pts',(-19.3672397192858,17.1909147664626,
3.75163935334847));
#194589=CARTESIAN_POINT('Ctrl Pts',(-19.3606327510181,17.1888555228621,
3.7512239590788));
#194590=CARTESIAN_POINT('Ctrl Pts',(-19.3435839467035,17.1836333713012,
3.75015091805408));
#194591=CARTESIAN_POINT('Ctrl Pts',(-19.3331276393709,17.180518751625,3.74949169987412));
#194592=CARTESIAN_POINT('Ctrl Pts',(-19.2888347996529,17.1676971654686,
3.74669429028345));
#194593=CARTESIAN_POINT('Ctrl Pts',(-19.2547845747077,17.1587545659254,
3.74453143921429));
#194594=CARTESIAN_POINT('Ctrl Pts',(-19.1649553149611,17.1375422254497,
3.73878997100111));
#194595=CARTESIAN_POINT('Ctrl Pts',(-19.1088779416,17.1266739102755,3.73516966847652));
#194596=CARTESIAN_POINT('Ctrl Pts',(-18.9020441647172,17.095204476871,3.72170059516301));
#194597=CARTESIAN_POINT('Ctrl Pts',(-18.7496309251215,17.0886007852889,
3.71151325108821));
#194598=CARTESIAN_POINT('Ctrl Pts',(-18.5753891062997,17.0998301631692,
3.70010896947933));
#194599=CARTESIAN_POINT('Ctrl Pts',(-18.5529541797568,17.1016356510266,
3.6986461573074));
#194600=CARTESIAN_POINT('Ctrl Pts',(-18.4794302653382,17.1087343124674,
3.69387852895901));
#194601=CARTESIAN_POINT('Ctrl Pts',(-18.4285005517896,17.1155292187516,
3.69061756279996));
#194602=CARTESIAN_POINT('Ctrl Pts',(-18.3701007822128,17.1254956517456,
3.68696353540444));
#194603=CARTESIAN_POINT('Ctrl Pts',(-18.3623445992239,17.1268638972527,
3.68647999166459));
#194604=CARTESIAN_POINT('Ctrl Pts',(-18.3499899916602,17.1291145003275,
3.68571276483803));
#194605=CARTESIAN_POINT('Ctrl Pts',(-18.3453866325855,17.1299688681116,
3.68542755890813));
#194606=CARTESIAN_POINT('Ctrl Pts',(-18.3372556552558,17.1315058705807,
3.68492501749278));
#194607=CARTESIAN_POINT('Ctrl Pts',(-18.3337268924935,17.1321822231061,
3.68470732836511));
#194608=CARTESIAN_POINT('Ctrl Pts',(-18.3262699935258,17.1336311670206,
3.68424819218868));
#194609=CARTESIAN_POINT('Ctrl Pts',(-18.3223423291099,17.1344059161639,
3.68400686977246));
#194610=CARTESIAN_POINT('Ctrl Pts',(-18.3117892200099,17.1365186808967,
3.68335978788533));
#194611=CARTESIAN_POINT('Ctrl Pts',(-18.3051678819098,17.1378773062455,
3.68295518879082));
#194612=CARTESIAN_POINT('Ctrl Pts',(-18.2728625195408,17.1446674068323,
3.68098749916396));
#194613=CARTESIAN_POINT('Ctrl Pts',(-18.2472732977086,17.1505448508723,
3.67944848146252));
#194614=CARTESIAN_POINT('Ctrl Pts',(-18.1742854569501,17.1687447493238,
3.67509796353542));
#194615=CARTESIAN_POINT('Ctrl Pts',(-18.1271943317503,17.1822382124924,
3.67233871987648));
#194616=CARTESIAN_POINT('Ctrl Pts',(-17.988708883323,17.2271740611538,3.66425503086561));
#194617=CARTESIAN_POINT('Ctrl Pts',(-17.8989529657018,17.263252042426,3.65905221383546));
#194618=CARTESIAN_POINT('Ctrl Pts',(-17.6850100182676,17.3667651877693,
3.64611957534623));
#194619=CARTESIAN_POINT('Ctrl Pts',(-17.5645222591219,17.4407185800776,
3.63833998948033));
#194620=CARTESIAN_POINT('Ctrl Pts',(-17.440920997773,17.5347423537324,3.62924197715143));
#194621=CARTESIAN_POINT('Ctrl Pts',(-17.4296413193198,17.5435044468074,
3.62840087284816));
#194622=CARTESIAN_POINT('Ctrl Pts',(-17.411828880737,17.5576325334598,3.62705481820785));
#194623=CARTESIAN_POINT('Ctrl Pts',(-17.4052379856689,17.5629247729135,
3.62655280543829));
#194624=CARTESIAN_POINT('Ctrl Pts',(-17.3936689366269,17.5723287922984,
3.6256645302439));
#194625=CARTESIAN_POINT('Ctrl Pts',(-17.3886775402258,17.5764241638287,
3.62527893318531));
#194626=CARTESIAN_POINT('Ctrl Pts',(-17.3783915692997,17.5849426889457,
3.62447938510047));
#194627=CARTESIAN_POINT('Ctrl Pts',(-17.3730997318831,17.5893690140154,
3.62406530736619));
#194628=CARTESIAN_POINT('Ctrl Pts',(-17.3595698527088,17.6007988683725,
3.62299951522317));
#194629=CARTESIAN_POINT('Ctrl Pts',(-17.3513637353089,17.6078397251536,
3.62234626975066));
#194630=CARTESIAN_POINT('Ctrl Pts',(-17.3173218762173,17.6375034583948,
3.61960740266274));
#194631=CARTESIAN_POINT('Ctrl Pts',(-17.2919857721781,17.660689378659,3.61749838980813));
#194632=CARTESIAN_POINT('Ctrl Pts',(-17.2274344851288,17.7227142261806,
3.61193382348519));
#194633=CARTESIAN_POINT('Ctrl Pts',(-17.1891562244276,17.7624865965264,
3.60843971050327));
#194634=CARTESIAN_POINT('Ctrl Pts',(-17.0797128785038,17.8854794597193,
3.59785667723224));
#194635=CARTESIAN_POINT('Ctrl Pts',(-17.013404858041,17.9727675999785,3.59061941136421));
#194636=CARTESIAN_POINT('Ctrl Pts',(-16.9252733487927,18.1096186290764,
3.57986716272942));
#194637=CARTESIAN_POINT('Ctrl Pts',(-16.8981025949038,18.1555313458928,
3.57635221990293));
#194638=CARTESIAN_POINT('Ctrl Pts',(-16.8666875789495,18.213507007949,3.57206079716307));
#194639=CARTESIAN_POINT('Ctrl Pts',(-16.8607802235557,18.2246452841926,
3.57124286633408));
#194640=CARTESIAN_POINT('Ctrl Pts',(-16.830403543619,18.2831775952021,3.56698088221409));
#194641=CARTESIAN_POINT('Ctrl Pts',(-16.8076300467672,18.331435492361,3.5635902492921));
#194642=CARTESIAN_POINT('Ctrl Pts',(-16.7832814460662,18.3885268069515,
3.55976151111705));
#194643=CARTESIAN_POINT('Ctrl Pts',(-16.7799103196028,18.396568568314,3.55922633472176));
#194644=CARTESIAN_POINT('Ctrl Pts',(-16.7748813066296,18.4087761889134,
3.55842041456937));
#194645=CARTESIAN_POINT('Ctrl Pts',(-16.773186855971,18.4129267496989,3.55814753426138));
#194646=CARTESIAN_POINT('Ctrl Pts',(-16.7701690500042,18.4203865032507,
3.55765915757875));
#194647=CARTESIAN_POINT('Ctrl Pts',(-16.7688408608608,18.4236936683568,
3.55744337310531));
#194648=CARTESIAN_POINT('Ctrl Pts',(-16.7659730596671,18.4308869099378,
3.55697561975071));
#194649=CARTESIAN_POINT('Ctrl Pts',(-16.7644366080456,18.4347741843195,
3.55672384190667));
#194650=CARTESIAN_POINT('Ctrl Pts',(-16.760153333913,18.445705610263,3.55601855091234));
#194651=CARTESIAN_POINT('Ctrl Pts',(-16.757432688094,18.4527600448411,3.55556658370545));
#194652=CARTESIAN_POINT('Ctrl Pts',(-16.7413975721506,18.4950107529676,
3.55287776383636));
#194653=CARTESIAN_POINT('Ctrl Pts',(-16.7289847772557,18.5305447203492,
3.55069131272691));
#194654=CARTESIAN_POINT('Ctrl Pts',(-16.6912622741091,18.6485491686528,
3.543616671411));
#194655=CARTESIAN_POINT('Ctrl Pts',(-16.6700426742774,18.7322402854818,
3.53889178941334));
#194656=CARTESIAN_POINT('Ctrl Pts',(-16.6211280727965,18.990470157116,3.52458895915509));
#194657=CARTESIAN_POINT('Ctrl Pts',(-16.6101004765044,19.1673495945278,
3.51510219294579));
#194658=CARTESIAN_POINT('Ctrl Pts',(-16.6225876545883,19.3664088391931,
3.50351150892648));
#194659=CARTESIAN_POINT('Ctrl Pts',(-16.6243933011252,19.3892512704385,
3.50216907549365));
#194660=CARTESIAN_POINT('Ctrl Pts',(-16.6274747076475,19.4215494630727,
3.5002516475308));
#194661=CARTESIAN_POINT('Ctrl Pts',(-16.628444202406,19.4310333211593,3.49968626697525));
#194662=CARTESIAN_POINT('Ctrl Pts',(-16.6301243411273,19.4464395624773,
3.4987638693762));
#194663=CARTESIAN_POINT('Ctrl Pts',(-16.6307960234147,19.4523661271407,
3.49840808334582));
#194664=CARTESIAN_POINT('Ctrl Pts',(-16.6322551296475,19.4647717433327,
3.49766131468196));
#194665=CARTESIAN_POINT('Ctrl Pts',(-16.6330474873899,19.4712501412938,
3.4972701799488));
#194666=CARTESIAN_POINT('Ctrl Pts',(-16.6350051359181,19.4866642239923,
3.49633674048221));
#194667=CARTESIAN_POINT('Ctrl Pts',(-16.6361975411364,19.4955962815855,
3.4957935843909));
#194668=CARTESIAN_POINT('Ctrl Pts',(-16.6404140880412,19.5257141744831,
3.49395436811252));
#194669=CARTESIAN_POINT('Ctrl Pts',(-16.6437023615917,19.5468611505771,
3.49264999269345));
#194670=CARTESIAN_POINT('Ctrl Pts',(-16.6634083595606,19.6620588842719,
3.48547106622526));
#194671=CARTESIAN_POINT('Ctrl Pts',(-16.6858512622676,19.7549543611588,
3.47940650833344));
#194672=CARTESIAN_POINT('Ctrl Pts',(-16.7656092587515,20.0086087244211,
3.46212616343468));
#194673=CARTESIAN_POINT('Ctrl Pts',(-16.8361823793679,20.1644290686028,
3.45062579842278));
#194674=CARTESIAN_POINT('Ctrl Pts',(-16.943705152627,20.3414324383234,3.43740901693797));
#194675=CARTESIAN_POINT('Ctrl Pts',(-16.9635516135627,20.37226914308,3.43510302750022));
#194676=CARTESIAN_POINT('Ctrl Pts',(-16.9882058697753,20.4084734861957,
3.43240575397968));
#194677=CARTESIAN_POINT('Ctrl Pts',(-16.9922512190136,20.4143499418328,
3.43196827865283));
#194678=CARTESIAN_POINT('Ctrl Pts',(-16.9989022926969,20.4239077812208,
3.43125742895086));
#194679=CARTESIAN_POINT('Ctrl Pts',(-17.0014901734997,20.4276014308657,
3.43098288842408));
#194680=CARTESIAN_POINT('Ctrl Pts',(-17.0061452649811,20.4342006088516,
3.4304927317174));
#194681=CARTESIAN_POINT('Ctrl Pts',(-17.0082080233292,20.4371091993318,
3.43027681818018));
#194682=CARTESIAN_POINT('Ctrl Pts',(-17.0126930098357,20.4433995082745,
3.42981014222676));
#194683=CARTESIAN_POINT('Ctrl Pts',(-17.015117851103,20.4467792931065,3.42955956353027));
#194684=CARTESIAN_POINT('Ctrl Pts',(-17.0219237596647,20.4562066952139,
3.42886101118834));
#194685=CARTESIAN_POINT('Ctrl Pts',(-17.0263269376507,20.4622383795355,
3.42841453635099));
#194686=CARTESIAN_POINT('Ctrl Pts',(-17.0521734736523,20.4972536239808,
3.4258245441598));
#194687=CARTESIAN_POINT('Ctrl Pts',(-17.0743238979072,20.5257107801461,
3.42372721356036));
#194688=CARTESIAN_POINT('Ctrl Pts',(-17.1480757792327,20.6156248061067,
3.41707538730218));
#194689=CARTESIAN_POINT('Ctrl Pts',(-17.2024494011681,20.6747217138211,
3.41266267814509));
#194690=CARTESIAN_POINT('Ctrl Pts',(-17.3931628851355,20.8597067959543,
3.39817929573788));
#194691=CARTESIAN_POINT('Ctrl Pts',(-17.5426454244653,20.9707575157078,
3.3882600528732));
#194692=CARTESIAN_POINT('Ctrl Pts',(-17.724012075889,21.0716726984023,3.37618901940036));
#194693=CARTESIAN_POINT('Ctrl Pts',(-17.7435122676712,21.0821259965933,
3.37489208203068));
#194694=CARTESIAN_POINT('Ctrl Pts',(-17.7706916734237,21.0961518952964,
3.37308414836764));
#194695=CARTESIAN_POINT('Ctrl Pts',(-17.7782342751361,21.0999871562315,
3.37258240119048));
#194696=CARTESIAN_POINT('Ctrl Pts',(-17.7912345063099,21.1064997164791,
3.37171747298293));
#194697=CARTESIAN_POINT('Ctrl Pts',(-17.796681084978,21.1091989362607,3.37135506376575));
#194698=CARTESIAN_POINT('Ctrl Pts',(-17.8079295628955,21.1147132483312,
3.37060648763457));
#194699=CARTESIAN_POINT('Ctrl Pts',(-17.8137328453446,21.1175253601738,
3.37022022166074));
#194700=CARTESIAN_POINT('Ctrl Pts',(-17.8272607880999,21.1240044742167,
3.36931961415898));
#194701=CARTESIAN_POINT('Ctrl Pts',(-17.8349949570232,21.1276512583466,
3.36880457797297));
#194702=CARTESIAN_POINT('Ctrl Pts',(-17.8597932596405,21.1391609328035,
3.36715262518793));
#194703=CARTESIAN_POINT('Ctrl Pts',(-17.8769396957805,21.1468433838744,
3.36600952837221));
#194704=CARTESIAN_POINT('Ctrl Pts',(-17.962940013082,21.1840092514451,3.36027031371747));
#194705=CARTESIAN_POINT('Ctrl Pts',(-18.0332152737659,21.2100491847617,
3.35555917983213));
#194706=CARTESIAN_POINT('Ctrl Pts',(-18.2086822873976,21.2646764370667,
3.34375254227823));
#194707=CARTESIAN_POINT('Ctrl Pts',(-18.3149835358247,21.2889719274676,
3.33655667270851));
#194708=CARTESIAN_POINT('Ctrl Pts',(-18.5412481554534,21.3226123840721,
3.32144440415869));
#194709=CARTESIAN_POINT('Ctrl Pts',(-18.6611220247945,21.3301402961569,
3.313555838931));
#194710=CARTESIAN_POINT('Ctrl Pts',(-18.7905135122365,21.3272669435106,
3.30556200239142));
#194711=CARTESIAN_POINT('Ctrl Pts',(-18.8000257874368,21.326991530329,3.3049774456643));
#194712=CARTESIAN_POINT('Ctrl Pts',(-18.814117734892,21.3264883991271,3.30411639140283));
#194713=CARTESIAN_POINT('Ctrl Pts',(-18.8186988924786,21.3263099339841,
3.30383724430556));
#194714=CARTESIAN_POINT('Ctrl Pts',(-18.826848459626,21.3259659391652,3.30334208047868));
#194715=CARTESIAN_POINT('Ctrl Pts',(-18.8304170587594,21.3258062586729,
3.30312574079422));
#194716=CARTESIAN_POINT('Ctrl Pts',(-18.8380882652773,21.325443544964,3.3026617431343));
#194717=CARTESIAN_POINT('Ctrl Pts',(-18.8421906789341,21.3252376047784,
3.3024142497511));
#194718=CARTESIAN_POINT('Ctrl Pts',(-18.8535122121464,21.3246362275369,
3.30173294931598));
#194719=CARTESIAN_POINT('Ctrl Pts',(-18.8607300236011,21.3242157428328,
3.30130052341879));
#194720=CARTESIAN_POINT('Ctrl Pts',(-18.9002465976868,21.3217104522226,
3.29894289595577));
#194721=CARTESIAN_POINT('Ctrl Pts',(-18.932498340221,21.3189220126568,3.29705473484988));
#194722=CARTESIAN_POINT('Ctrl Pts',(-19.1265309786929,21.2976529281723,
3.28584523796555));
#194723=CARTESIAN_POINT('Ctrl Pts',(-19.2858160989885,21.2612955665585,
3.27723919543386));
#194724=CARTESIAN_POINT('Ctrl Pts',(-19.5495590289864,21.1680922258782,
3.26192580803239));
#194725=CARTESIAN_POINT('Ctrl Pts',(-19.6563184295678,21.1201018730927,
3.2554019306277));
#194726=CARTESIAN_POINT('Ctrl Pts',(-19.7721865477171,21.0560203156677,
3.24764514155896));
#194727=CARTESIAN_POINT('Ctrl Pts',(-19.7857235678568,21.0483374188237,
3.24672812929792));
#194728=CARTESIAN_POINT('Ctrl Pts',(-19.8061729231246,21.0364314026384,
3.24532584619987));
#194729=CARTESIAN_POINT('Ctrl Pts',(-19.8131479585771,21.0323166291268,
3.24484449444167));
#194730=CARTESIAN_POINT('Ctrl Pts',(-19.8254396220627,21.0249700275085,
3.24399075270369));
#194731=CARTESIAN_POINT('Ctrl Pts',(-19.8307659624935,21.0217545751831,
3.24361896378203));
#194732=CARTESIAN_POINT('Ctrl Pts',(-19.8420026163977,21.0149033655167,
3.24283068947592));
#194733=CARTESIAN_POINT('Ctrl Pts',(-19.8479093728519,21.0112619413171,
3.24241399870618));
#194734=CARTESIAN_POINT('Ctrl Pts',(-19.8599605117035,21.0037505836147,
3.2415590477976));
#194735=CARTESIAN_POINT('Ctrl Pts',(-19.866103093518,20.9998779479206,3.24112069126428));
#194736=CARTESIAN_POINT('Ctrl Pts',(-19.8812445575404,20.9902226794257,
3.24003368758007));
#194737=CARTESIAN_POINT('Ctrl Pts',(-19.8902196935948,20.9844033470528,
3.23938368072231));
#194738=CARTESIAN_POINT('Ctrl Pts',(-19.9967259000512,20.9141942478109,
3.23160138067261));
#194739=CARTESIAN_POINT('Ctrl Pts',(-20.0887916533393,20.841913572239,3.22416485619098));
#194740=CARTESIAN_POINT('Ctrl Pts',(-20.3104130479253,20.6361493847985,
3.20441973838464));
#194741=CARTESIAN_POINT('Ctrl Pts',(-20.4292177876253,20.4925488607579,
3.19185582995532));
#194742=CARTESIAN_POINT('Ctrl Pts',(-20.5353383515891,20.3232372822493,
3.17941620880226));
#194743=CARTESIAN_POINT('Ctrl Pts',(-20.5427765658817,20.3110995358283,
3.17853674385243));
#194744=CARTESIAN_POINT('Ctrl Pts',(-20.5529509485145,20.294114674696,3.1773240990047));
#194745=CARTESIAN_POINT('Ctrl Pts',(-20.5557911003333,20.289330719214,3.17698451330051));
#194746=CARTESIAN_POINT('Ctrl Pts',(-20.5603198446551,20.2816335330842,
3.17644135553094));
#194747=CARTESIAN_POINT('Ctrl Pts',(-20.5620203804379,20.2787274119442,
3.17623701625981));
#194748=CARTESIAN_POINT('Ctrl Pts',(-20.565558136712,20.2726483572403,3.17581112739224));
#194749=CARTESIAN_POINT('Ctrl Pts',(-20.5673940540597,20.2694746975455,
3.1755896669461));
#194750=CARTESIAN_POINT('Ctrl Pts',(-20.5718153760083,20.2617857609393,
3.17505521769718));
#194751=CARTESIAN_POINT('Ctrl Pts',(-20.574392419023,20.2572656531684,3.17474276745335));
#194752=CARTESIAN_POINT('Ctrl Pts',(-20.583349174217,20.2414201063898,3.17365335283475));
#194753=CARTESIAN_POINT('Ctrl Pts',(-20.5896413683298,20.2300451878635,
3.17288180901761));
#194754=CARTESIAN_POINT('Ctrl Pts',(-20.626171071982,20.1625469869171,3.1683609097762));
#194755=CARTESIAN_POINT('Ctrl Pts',(-20.6539686038732,20.1051337403328,
3.16474776973187));
#194756=CARTESIAN_POINT('Ctrl Pts',(-20.6946425036429,20.0104459608017,
3.15901977670304));
#194757=CARTESIAN_POINT('Ctrl Pts',(-20.7091282699385,19.973951900444,3.15686533709011));
#194758=CARTESIAN_POINT('Ctrl Pts',(-20.7225806782367,19.9371101060747,
3.15472451729435));
#194759=CARTESIAN_POINT('Ctrl Pts',(-20.722580576248,19.9371103853886,2.93545682861291));
#194760=CARTESIAN_POINT('Ctrl Pts',(-20.674294176734,20.0693511549778,2.94352078684689));
#194761=CARTESIAN_POINT('Ctrl Pts',(-20.6129098886537,20.1965203883229,
2.95104140375662));
#194762=CARTESIAN_POINT('Ctrl Pts',(-20.4906188222878,20.3961859327918,
2.96379346074783));
#194763=CARTESIAN_POINT('Ctrl Pts',(-20.436747863976,20.4723576225925,2.96891787851721));
#194764=CARTESIAN_POINT('Ctrl Pts',(-20.3470885818636,20.5828773470361,
2.97700806590996));
#194765=CARTESIAN_POINT('Ctrl Pts',(-20.3148231570149,20.6199357057277,
2.97984502488194));
#194766=CARTESIAN_POINT('Ctrl Pts',(-20.2731171368074,20.6645993893865,
2.98344130758929));
#194767=CARTESIAN_POINT('Ctrl Pts',(-20.2648603003467,20.6732925417145,
2.98414999872162));
#194768=CARTESIAN_POINT('Ctrl Pts',(-20.2514581381414,20.6871649933568,
2.98529531847376));
#194769=CARTESIAN_POINT('Ctrl Pts',(-20.2463590115715,20.6923887088454,
2.98572993655263));
#194770=CARTESIAN_POINT('Ctrl Pts',(-20.23676208271,20.7021189289957,2.98654584958489));
#194771=CARTESIAN_POINT('Ctrl Pts',(-20.2322707588035,20.7066317292645,
2.98692685684658));
#194772=CARTESIAN_POINT('Ctrl Pts',(-20.2221914699005,20.7166682520657,
2.98778008146402));
#194773=CARTESIAN_POINT('Ctrl Pts',(-20.216592993948,20.7221812426254,2.98825276457139));
#194774=CARTESIAN_POINT('Ctrl Pts',(-20.2023627094792,20.7360390473774,
2.98945120931347));
#194775=CARTESIAN_POINT('Ctrl Pts',(-20.1936904475494,20.7443417527191,
2.99017878883542));
#194776=CARTESIAN_POINT('Ctrl Pts',(-20.1444074798519,20.7907275974345,
2.99429845813934));
#194777=CARTESIAN_POINT('Ctrl Pts',(-20.1023806877526,20.8272679005677,
2.99775552007251));
#194778=CARTESIAN_POINT('Ctrl Pts',(-20.0362234156259,20.8803571973296,
3.00311869446364));
#194779=CARTESIAN_POINT('Ctrl Pts',(-20.0131072879826,20.8981347627081,
3.00497872929123));
#194780=CARTESIAN_POINT('Ctrl Pts',(-19.8632098503749,21.0085624056929,
3.01694731135086));
#194781=CARTESIAN_POINT('Ctrl Pts',(-19.7268213345117,21.087337798399,3.02747187506542));
#194782=CARTESIAN_POINT('Ctrl Pts',(-19.5380931236786,21.1699605503791,
3.04091643176587));
#194783=CARTESIAN_POINT('Ctrl Pts',(-19.4925132432654,21.1880560144762,
3.04408012381068));
#194784=CARTESIAN_POINT('Ctrl Pts',(-19.4216037413538,21.21339364062,3.04883525114068));
#194785=CARTESIAN_POINT('Ctrl Pts',(-19.396700328173,21.2217728909936,3.05047441617128));
#194786=CARTESIAN_POINT('Ctrl Pts',(-19.3651992312652,21.2317231971571,
3.05250371074648));
#194787=CARTESIAN_POINT('Ctrl Pts',(-19.3587425359735,21.2337287202385,
3.05291733842175));
#194788=CARTESIAN_POINT('Ctrl Pts',(-19.3484471159471,21.236872594996,3.05357308254486));
#194789=CARTESIAN_POINT('Ctrl Pts',(-19.3446146419496,21.238031028155,3.05381634801302));
#194790=CARTESIAN_POINT('Ctrl Pts',(-19.3373366954821,21.2402084025413,
3.05427669907735));
#194791=CARTESIAN_POINT('Ctrl Pts',(-19.3338919591473,21.2412294320012,
3.05449389977425));
#194792=CARTESIAN_POINT('Ctrl Pts',(-19.3259529986308,21.2435605922227,
3.05499291352776));
#194793=CARTESIAN_POINT('Ctrl Pts',(-19.3214570183267,21.2448645889602,
3.0552743670054));
#194794=CARTESIAN_POINT('Ctrl Pts',(-19.3093877749042,21.2483217462275,
3.05602693294367));
#194795=CARTESIAN_POINT('Ctrl Pts',(-19.3018066807179,21.2504476131665,
3.0564965020632));
#194796=CARTESIAN_POINT('Ctrl Pts',(-19.2447447455184,21.26610590057,3.06000852757599));
#194797=CARTESIAN_POINT('Ctrl Pts',(-19.1947942449952,21.2778792994095,
3.0629568649243));
#194798=CARTESIAN_POINT('Ctrl Pts',(-19.1224217189075,21.2921829039909,
3.06711287204316));
#194799=CARTESIAN_POINT('Ctrl Pts',(-19.1003137572517,21.296187759523,3.06836708465605));
#194800=CARTESIAN_POINT('Ctrl Pts',(-18.9306983870196,21.3241326484922,
3.0778999644202));
#194801=CARTESIAN_POINT('Ctrl Pts',(-18.7810920699222,21.3327457862096,
3.08582264540635));
#194802=CARTESIAN_POINT('Ctrl Pts',(-18.5729911334362,21.3226898906018,
3.09737307806423));
#194803=CARTESIAN_POINT('Ctrl Pts',(-18.5143091689989,21.3173934164892,
3.1006850253826));
#194804=CARTESIAN_POINT('Ctrl Pts',(-18.4202434092413,21.3049296775668,
3.10613622209162));
#194805=CARTESIAN_POINT('Ctrl Pts',(-18.3846876387832,21.2992924462735,
3.1082296202063));
#194806=CARTESIAN_POINT('Ctrl Pts',(-18.3384789537933,21.2907531269146,
3.11100018952998));
#194807=CARTESIAN_POINT('Ctrl Pts',(-18.327679482196,21.2886702329314,3.11165127876057));
#194808=CARTESIAN_POINT('Ctrl Pts',(-18.3100930298703,21.2851359749784,
3.11271757899035));
#194809=CARTESIAN_POINT('Ctrl Pts',(-18.3032960045519,21.283735204643,3.11313116986443));
#194810=CARTESIAN_POINT('Ctrl Pts',(-18.2902040403987,21.2809699595375,
3.11393069502366));
#194811=CARTESIAN_POINT('Ctrl Pts',(-18.2839081919858,21.2796101252007,
3.11431647658929));
#194812=CARTESIAN_POINT('Ctrl Pts',(-18.2694591468087,21.2764202039866,
3.11520486932457));
#194813=CARTESIAN_POINT('Ctrl Pts',(-18.261310422863,21.2745705424964,3.11570810438923));
#194814=CARTESIAN_POINT('Ctrl Pts',(-18.2395866276593,21.2695040795906,
3.11705570048035));
#194815=CARTESIAN_POINT('Ctrl Pts',(-18.2260322191464,21.2662012912196,
3.11790281510485));
#194816=CARTESIAN_POINT('Ctrl Pts',(-18.1175031400767,21.238616918699,3.12473726981985));
#194817=CARTESIAN_POINT('Ctrl Pts',(-18.0243000911508,21.2079026180012,
3.13093375870797));
#194818=CARTESIAN_POINT('Ctrl Pts',(-17.8056468900667,21.1186014984214,
3.14624081667651));
#194819=CARTESIAN_POINT('Ctrl Pts',(-17.6831482769317,21.0539568216178,
3.15548273967279));
#194820=CARTESIAN_POINT('Ctrl Pts',(-17.5257609959178,20.9500769915515,
3.16779961637272));
#194821=CARTESIAN_POINT('Ctrl Pts',(-17.484690354188,20.9208117909914,3.17105608982906));
#194822=CARTESIAN_POINT('Ctrl Pts',(-17.4234655035585,20.87380040142,3.17593322307956));
#194823=CARTESIAN_POINT('Ctrl Pts',(-17.4025397620007,20.8570922304318,
3.17760435836788));
#194824=CARTESIAN_POINT('Ctrl Pts',(-17.3767001964428,20.8356453563956,
3.17966734726269));
#194825=CARTESIAN_POINT('Ctrl Pts',(-17.3714857501643,20.831274733709,3.18008362940935));
#194826=CARTESIAN_POINT('Ctrl Pts',(-17.3632291431778,20.8242862002877,
3.18074259907813));
#194827=CARTESIAN_POINT('Ctrl Pts',(-17.3601732515484,20.8216846903756,
3.18098645482183));
#194828=CARTESIAN_POINT('Ctrl Pts',(-17.3543974108886,20.8167392651717,
3.18144725404704));
#194829=CARTESIAN_POINT('Ctrl Pts',(-17.351676061376,20.8143971499484,3.18166431634587));
#194830=CARTESIAN_POINT('Ctrl Pts',(-17.3454335868465,20.8089968917271,
3.18216214558974));
#194831=CARTESIAN_POINT('Ctrl Pts',(-17.3419166016,20.8059340307859,3.18244255872497));
#194832=CARTESIAN_POINT('Ctrl Pts',(-17.3325346538488,20.797708835855,3.18319051609213));
#194833=CARTESIAN_POINT('Ctrl Pts',(-17.3266880368958,20.7925255574938,
3.18365654647553));
#194834=CARTESIAN_POINT('Ctrl Pts',(-17.2837642380047,20.7540452434154,
3.18707855710478));
#194835=CARTESIAN_POINT('Ctrl Pts',(-17.2478412208922,20.7194778153257,
3.18994575535038));
#194836=CARTESIAN_POINT('Ctrl Pts',(-17.1654590508402,20.634401587934,3.19662582273113));
#194837=CARTESIAN_POINT('Ctrl Pts',(-17.1201687782878,20.5828391432208,
3.20038544235283));
#194838=CARTESIAN_POINT('Ctrl Pts',(-17.0090836959537,20.443238452875,3.21010125503683));
#194839=CARTESIAN_POINT('Ctrl Pts',(-16.9474996018098,20.3521237263023,
3.21601186210985));
#194840=CARTESIAN_POINT('Ctrl Pts',(-16.8555144959244,20.1901944028768,
3.22636238890177));
#194841=CARTESIAN_POINT('Ctrl Pts',(-16.8213964512187,20.1217553714144,
3.23069281713936));
#194842=CARTESIAN_POINT('Ctrl Pts',(-16.7835125838982,20.0341941506857,
3.23626232229619));
#194843=CARTESIAN_POINT('Ctrl Pts',(-16.7762055319999,20.0166615644226,
3.23737875004261));
#194844=CARTESIAN_POINT('Ctrl Pts',(-16.7659385590013,19.9910621302361,
3.23901160114075));
#194845=CARTESIAN_POINT('Ctrl Pts',(-16.7627901397617,19.9830715291721,
3.23952166181124));
#194846=CARTESIAN_POINT('Ctrl Pts',(-16.7573608850013,19.9690425258735,
3.24041792940939));
#194847=CARTESIAN_POINT('Ctrl Pts',(-16.7550588668143,19.9630124014517,
3.24080341896293));
#194848=CARTESIAN_POINT('Ctrl Pts',(-16.75064636719,19.951293310164,3.24155310059979));
#194849=CARTESIAN_POINT('Ctrl Pts',(-16.7485326947236,19.9456056059824,
3.24191718127886));
#194850=CARTESIAN_POINT('Ctrl Pts',(-16.7435444058367,19.9320037616824,
3.24278845134586));
#194851=CARTESIAN_POINT('Ctrl Pts',(-16.7406925124986,19.9240814495994,
3.24329639292468));
#194852=CARTESIAN_POINT('Ctrl Pts',(-16.7306063846141,19.8955297126004,
3.24512882906657));
#194853=CARTESIAN_POINT('Ctrl Pts',(-16.7236447255072,19.8748060858997,
3.24646230673773));
#194854=CARTESIAN_POINT('Ctrl Pts',(-16.6599021177827,19.6748485423855,
3.25936579453176));
#194855=CARTESIAN_POINT('Ctrl Pts',(-16.6269267470173,19.4889408487993,
3.27175923197078));
#194856=CARTESIAN_POINT('Ctrl Pts',(-16.6155745605528,19.2226745827203,
3.28935021725087));
#194857=CARTESIAN_POINT('Ctrl Pts',(-16.6166004195378,19.1440423965755,
3.29450882005877));
#194858=CARTESIAN_POINT('Ctrl Pts',(-16.6244404954491,19.0301265169542,
3.30178495156751));
#194859=CARTESIAN_POINT('Ctrl Pts',(-16.6277807474953,18.9946731015927,
3.30402109499804));
#194860=CARTESIAN_POINT('Ctrl Pts',(-16.632898464929,18.9519310986414,3.30666931684317));
#194861=CARTESIAN_POINT('Ctrl Pts',(-16.6338219515318,18.9445482692111,
3.3071250166315));
#194862=CARTESIAN_POINT('Ctrl Pts',(-16.6353216182513,18.9330516190588,
3.30783178271872));
#194863=CARTESIAN_POINT('Ctrl Pts',(-16.6358710052018,18.9289344502446,
3.30808431743661));
#194864=CARTESIAN_POINT('Ctrl Pts',(-16.6369146307297,18.921285185992,3.308552403415));
#194865=CARTESIAN_POINT('Ctrl Pts',(-16.6374056725163,18.9177527567096,
3.30876812636692));
#194866=CARTESIAN_POINT('Ctrl Pts',(-16.6385390401514,18.9097479803668,
3.30925599056532));
#194867=CARTESIAN_POINT('Ctrl Pts',(-16.6391867564605,18.9052764498054,
3.30952782390702));
#194868=CARTESIAN_POINT('Ctrl Pts',(-16.6408980490523,18.8937233031635,
3.31022845412401));
#194869=CARTESIAN_POINT('Ctrl Pts',(-16.6419832600324,18.8866448822526,
3.3106560572816));
#194870=CARTESIAN_POINT('Ctrl Pts',(-16.6489123648876,18.8429309095058,
3.31328727076249));
#194871=CARTESIAN_POINT('Ctrl Pts',(-16.6556828986259,18.8064462910856,
3.3154419838569));
#194872=CARTESIAN_POINT('Ctrl Pts',(-16.6988858517993,18.6035272364578,
3.32728797625059));
#194873=CARTESIAN_POINT('Ctrl Pts',(-16.754348967805,18.4417754020813,3.3362519566324));
#194874=CARTESIAN_POINT('Ctrl Pts',(-16.8700557848137,18.202810555408,3.35085875138092));
#194875=CARTESIAN_POINT('Ctrl Pts',(-16.9172191154571,18.120111298474,3.35619207864221));
#194876=CARTESIAN_POINT('Ctrl Pts',(-16.9815825874255,18.0230697251581,
3.36297297135718));
#194877=CARTESIAN_POINT('Ctrl Pts',(-16.9936556466916,18.005451739431,3.36422617644362));
#194878=CARTESIAN_POINT('Ctrl Pts',(-17.0111944269801,17.9806703574607,
3.36602208509113));
#194879=CARTESIAN_POINT('Ctrl Pts',(-17.0164427559218,17.9733541777877,
3.36655647648905));
#194880=CARTESIAN_POINT('Ctrl Pts',(-17.0255748574342,17.9607939719363,
3.36748126313192));
#194881=CARTESIAN_POINT('Ctrl Pts',(-17.0294365262826,17.9555339737945,
3.3678707991702));
#194882=CARTESIAN_POINT('Ctrl Pts',(-17.0368752960774,17.9454991769957,
3.36861830277713));
#194883=CARTESIAN_POINT('Ctrl Pts',(-17.0404483887357,17.9407214744236,
3.36897611140026));
#194884=CARTESIAN_POINT('Ctrl Pts',(-17.0497884292747,17.9283420453147,
3.36990824636289));
#194885=CARTESIAN_POINT('Ctrl Pts',(-17.0555866127161,17.9207641531851,
3.3704837985326));
#194886=CARTESIAN_POINT('Ctrl Pts',(-17.0755132229462,17.8950828473311,
3.37245148539138));
#194887=CARTESIAN_POINT('Ctrl Pts',(-17.0898845081516,17.8771707280767,
3.37385324225886));
#194888=CARTESIAN_POINT('Ctrl Pts',(-17.2168421286309,17.7241027822618,
3.38609352168608));
#194889=CARTESIAN_POINT('Ctrl Pts',(-17.3455575527169,17.6032576965896,
3.39763949798531));
#194890=CARTESIAN_POINT('Ctrl Pts',(-17.5577942539594,17.4486863111455,
3.41498664519782));
#194891=CARTESIAN_POINT('Ctrl Pts',(-17.6309697273569,17.4019849027498,
3.42070133631461));
#194892=CARTESIAN_POINT('Ctrl Pts',(-17.7398154831848,17.3415853470848,
3.42864839395857));
#194893=CARTESIAN_POINT('Ctrl Pts',(-17.7733096664698,17.324153824787,3.43102279981182));
#194894=CARTESIAN_POINT('Ctrl Pts',(-17.8140582895227,17.304313471832,3.43381170260923));
#194895=CARTESIAN_POINT('Ctrl Pts',(-17.820880005455,17.3010371346785,3.43427529405046));
#194896=CARTESIAN_POINT('Ctrl Pts',(-17.8314980692211,17.2960073763876,
3.43499160117533));
#194897=CARTESIAN_POINT('Ctrl Pts',(-17.8352822107371,17.2942285427026,
3.43524584879597));
#194898=CARTESIAN_POINT('Ctrl Pts',(-17.8423013457109,17.2909543727722,
3.43571549900468));
#194899=CARTESIAN_POINT('Ctrl Pts',(-17.8455348165529,17.2894560065411,
3.43593108340598));
#194900=CARTESIAN_POINT('Ctrl Pts',(-17.8528426877208,17.2860919836153,
3.43641660178693));
#194901=CARTESIAN_POINT('Ctrl Pts',(-17.8569192255296,17.2842310993717,
3.43668624035576));
#194902=CARTESIAN_POINT('Ctrl Pts',(-17.8689371416884,17.2787911279314,
3.43747772186595));
#194903=CARTESIAN_POINT('Ctrl Pts',(-17.8768948473473,17.2752480434398,
3.43799740599801));
#194904=CARTESIAN_POINT('Ctrl Pts',(-17.9335931305573,17.250421915488,3.44167052638591));
#194905=CARTESIAN_POINT('Ctrl Pts',(-17.9831029613884,17.2309312560237,
3.44472319528746));
#194906=CARTESIAN_POINT('Ctrl Pts',(-18.0354590603296,17.2125669144527,
3.44784390083105));
#194907=CARTESIAN_POINT('Ctrl Pts',(-18.0376207455991,17.2118126211102,
3.44797256035732));
#194908=CARTESIAN_POINT('Ctrl Pts',(-18.1790518309796,17.1627192178655,
3.45637820594238));
#194909=CARTESIAN_POINT('Ctrl Pts',(-18.3229953469071,17.1290532342067,
3.46419526710065));
#194910=CARTESIAN_POINT('Ctrl Pts',(-18.5662418109367,17.0983955015415,
3.4776670819938));
#194911=CARTESIAN_POINT('Ctrl Pts',(-18.6639259919915,17.0929048740995,
3.48313974083939));
#194912=CARTESIAN_POINT('Ctrl Pts',(-18.7832996905922,17.0944631927324,
3.49008947755054));
#194913=CARTESIAN_POINT('Ctrl Pts',(-18.8049599212159,17.0950786511952,
3.49136067086335));
#194914=CARTESIAN_POINT('Ctrl Pts',(-18.8356539834407,17.0964226226306,
3.49317790883942));
#194915=CARTESIAN_POINT('Ctrl Pts',(-18.8446989064189,17.0968768329473,
3.49371536572356));
#194916=CARTESIAN_POINT('Ctrl Pts',(-18.8602650117813,17.0977586857453,
3.49464378679632));
#194917=CARTESIAN_POINT('Ctrl Pts',(-18.8667876888746,17.0981585166701,
3.49503387357448));
#194918=CARTESIAN_POINT('Ctrl Pts',(-18.8792508340747,17.0989804305249,
3.49578127495249));
#194919=CARTESIAN_POINT('Ctrl Pts',(-18.8851915859044,17.0993973930044,
3.4961384250107));
#194920=CARTESIAN_POINT('Ctrl Pts',(-18.9005869113662,17.1005432435248,
3.49706631496793));
#194921=CARTESIAN_POINT('Ctrl Pts',(-18.9100384115632,17.1013105932226,
3.49763825862536));
#194922=CARTESIAN_POINT('Ctrl Pts',(-18.9420029627241,17.1041220301849,
3.49958048033892));
#194923=CARTESIAN_POINT('Ctrl Pts',(-18.9644877178414,17.1064631478775,
3.50096004589867));
#194924=CARTESIAN_POINT('Ctrl Pts',(-19.1659634924792,17.1307082673477,
3.51344597501258));
#194925=CARTESIAN_POINT('Ctrl Pts',(-19.3414786543945,17.1750357395059,
3.52530078801102));
#194926=CARTESIAN_POINT('Ctrl Pts',(-19.5870768084979,17.2716829728511,
3.5427338722436));
#194927=CARTESIAN_POINT('Ctrl Pts',(-19.6630604514825,17.3069151606001,
3.54824049257048));
#194928=CARTESIAN_POINT('Ctrl Pts',(-19.7693186012447,17.3640644743566,
3.55593788520325));
#194929=CARTESIAN_POINT('Ctrl Pts',(-19.8014122712448,17.3824249072294,
3.55826177967616));
#194930=CARTESIAN_POINT('Ctrl Pts',(-19.839439811248,17.4055226655027,3.5609993889357));
#194931=CARTESIAN_POINT('Ctrl Pts',(-19.845848123005,17.4094619524007,3.56146016395888));
#194932=CARTESIAN_POINT('Ctrl Pts',(-19.8557774347931,17.4156388140984,
3.56217306723734));
#194933=CARTESIAN_POINT('Ctrl Pts',(-19.859312973088,17.4178527348972,3.56242670462952));
#194934=CARTESIAN_POINT('Ctrl Pts',(-19.865857594475,17.421977894845,3.56289579358229));
#194935=CARTESIAN_POINT('Ctrl Pts',(-19.868868366988,17.4238862664055,3.56311142335979));
#194936=CARTESIAN_POINT('Ctrl Pts',(-19.8756640864316,17.4282178174308,
3.56359775932483));
#194937=CARTESIAN_POINT('Ctrl Pts',(-19.8794461357558,17.4306454432692,
3.56386816572663));
#194938=CARTESIAN_POINT('Ctrl Pts',(-19.8905863985753,17.4378463605746,
3.56466399626279));
#194939=CARTESIAN_POINT('Ctrl Pts',(-19.8979228154563,17.4426534242246,
3.56518722594247));
#194940=CARTESIAN_POINT('Ctrl Pts',(-19.9507592063296,17.4777448562216,
3.56895083887473));
#194941=CARTESIAN_POINT('Ctrl Pts',(-19.9951052480139,17.5097384087307,
3.5720847371227));
#194942=CARTESIAN_POINT('Ctrl Pts',(-20.1707478296543,17.6471031020045,
3.58461106230112));
#194943=CARTESIAN_POINT('Ctrl Pts',(-20.290496176468,17.7662353072659,3.59346952949677));
#194944=CARTESIAN_POINT('Ctrl Pts',(-20.4314204297724,17.944537890231,3.60606884571564));
#194945=CARTESIAN_POINT('Ctrl Pts',(-20.4660158001134,17.9922781716356,
3.6093827767193));
#194946=CARTESIAN_POINT('Ctrl Pts',(-20.5184688775535,18.0714138109634,
3.61483694415326));
#194947=CARTESIAN_POINT('Ctrl Pts',(-20.5375946862398,18.1019319954593,
3.61693126388929));
#194948=CARTESIAN_POINT('Ctrl Pts',(-20.5615339449738,18.1423888986536,
3.61970288369652));
#194949=CARTESIAN_POINT('Ctrl Pts',(-20.5670618559126,18.1518993289392,
3.62035407668547));
#194950=CARTESIAN_POINT('Ctrl Pts',(-20.5759561082204,18.1674795819698,
3.62142050424096));
#194951=CARTESIAN_POINT('Ctrl Pts',(-20.579367206134,18.1735237158283,3.62183411793738));
#194952=CARTESIAN_POINT('Ctrl Pts',(-20.5858865435777,18.185209224511,3.62263365735505));
#194953=CARTESIAN_POINT('Ctrl Pts',(-20.5889988830437,18.1908482329343,
3.62301943019648));
#194954=CARTESIAN_POINT('Ctrl Pts',(-20.5960893269204,18.2038345979843,
3.62390776015328));
#194955=CARTESIAN_POINT('Ctrl Pts',(-20.6000497457547,18.2111914424794,
3.62441094087385));
#194956=CARTESIAN_POINT('Ctrl Pts',(-20.6105050970159,18.2308917588406,
3.62575829686116));
#194957=CARTESIAN_POINT('Ctrl Pts',(-20.6169216820362,18.2432761405141,
3.62660522418123));
#194958=CARTESIAN_POINT('Ctrl Pts',(-20.6678619786731,18.3440188229043,
3.63349516759902));
#194959=CARTESIAN_POINT('Ctrl Pts',(-20.7062574655786,18.4353234214685,
3.63975142507013));
#194960=CARTESIAN_POINT('Ctrl Pts',(-20.7819939206222,18.6578717871092,
3.65499311512505));
#194961=CARTESIAN_POINT('Ctrl Pts',(-20.8133219835055,18.7907067361352,
3.66409682105377));
#194962=CARTESIAN_POINT('Ctrl Pts',(-20.8417530853864,18.9996855456632,
3.67787835293917));
#194963=CARTESIAN_POINT('Ctrl Pts',(-20.8479010431315,19.0742457273808,
3.68268516259665));
#194964=CARTESIAN_POINT('Ctrl Pts',(-20.8503509135253,19.1578371651599,
3.68784422392104));
#194965=CARTESIAN_POINT('Ctrl Pts',(-20.850554851592,19.1666937623867,3.68838793079842));
#194966=CARTESIAN_POINT('Ctrl Pts',(-20.8507777607909,19.1800041518406,
3.68920043427108));
#194967=CARTESIAN_POINT('Ctrl Pts',(-20.8508382796655,19.1844570204453,
3.68947147272052));
#194968=CARTESIAN_POINT('Ctrl Pts',(-20.8509183443664,19.1921296534542,
3.68993711501611));
#194969=CARTESIAN_POINT('Ctrl Pts',(-20.8509445959975,19.1953492924698,
3.6901320912159));
#194970=CARTESIAN_POINT('Ctrl Pts',(-20.850987402342,19.2026391165335,3.69057259526842));
#194971=CARTESIAN_POINT('Ctrl Pts',(-20.8509995645895,19.2067092871484,
3.69081787437903));
#194972=CARTESIAN_POINT('Ctrl Pts',(-20.8510007238771,19.2178398475239,
3.69148685974545));
#194973=CARTESIAN_POINT('Ctrl Pts',(-20.8509661391612,19.2249002609865,
3.6919092662087));
#194974=CARTESIAN_POINT('Ctrl Pts',(-20.8505991940585,19.2619597474054,
3.69411682418592));
#194975=CARTESIAN_POINT('Ctrl Pts',(-20.8496644767133,19.2919510627868,
3.69587027679547));
#194976=CARTESIAN_POINT('Ctrl Pts',(-20.8449576393496,19.3816663716478,
3.70104321441789));
#194977=CARTESIAN_POINT('Ctrl Pts',(-20.8392907084485,19.4412633856781,
3.7043837998999));
#194978=CARTESIAN_POINT('Ctrl Pts',(-20.8105321382441,19.6495555519041,
3.71596096917035));
#194979=CARTESIAN_POINT('Ctrl Pts',(-20.7741427280388,19.7958983757255,
3.72394896228244));
#194980=CARTESIAN_POINT('Ctrl Pts',(-20.7225806064494,19.9371103026766,
3.73234504707874));
#194981=CARTESIAN_POINT('Origin',(-18.734,19.211,0.));
#194982=CARTESIAN_POINT('',(-20.7225806084094,19.937110297309,4.75730094873459));
#194983=CARTESIAN_POINT('',(-20.7225805792317,19.9371103772171,4.53222349041431));
#194984=CARTESIAN_POINT('',(-20.7225806064498,19.9371103026755,0.));
#194985=CARTESIAN_POINT('',(-20.8509999221905,19.2104260266189,4.70909172043352));
#194986=CARTESIAN_POINT('Ctrl Pts',(-20.7225806084094,19.937110297309,4.75730094873459));
#194987=CARTESIAN_POINT('Ctrl Pts',(-20.7382263485064,19.8942616894923,
4.75443866810734));
#194988=CARTESIAN_POINT('Ctrl Pts',(-20.7524832949378,19.8509180613671,
4.75153426385756));
#194989=CARTESIAN_POINT('Ctrl Pts',(-20.8222129884855,19.6133189441214,
4.73557997940159));
#194990=CARTESIAN_POINT('Ctrl Pts',(-20.8510546775763,19.4123816420812,
4.72184240933827));
#194991=CARTESIAN_POINT('Ctrl Pts',(-20.8509999221905,19.2104260266189,
4.70909172043352));
#194992=CARTESIAN_POINT('Ctrl Pts',(-20.8509999215531,19.2104236806784,
4.70909157232004));
#194993=CARTESIAN_POINT('Ctrl Pts',(-20.8509956361906,19.1946822127091,
4.70809771821267));
#194994=CARTESIAN_POINT('Ctrl Pts',(-20.8508157764336,19.1789407168608,
4.70711098890863));
#194995=CARTESIAN_POINT('Ctrl Pts',(-20.8502148552955,19.1523322896803,
4.70545674230044));
#194996=CARTESIAN_POINT('Ctrl Pts',(-20.849885630565,19.1414642283405,4.704784929544));
#194997=CARTESIAN_POINT('Ctrl Pts',(-20.8492914997428,19.1258317551766,
4.70382461278879));
#194998=CARTESIAN_POINT('Ctrl Pts',(-20.8490942018603,19.1210651509873,
4.7035326004156));
#194999=CARTESIAN_POINT('Ctrl Pts',(-20.8487208813721,19.112728068835,4.70302330825673));
#195000=CARTESIAN_POINT('Ctrl Pts',(-20.8485519257395,19.1091573156752,
4.70280564676389));
#195001=CARTESIAN_POINT('Ctrl Pts',(-20.8482044716945,19.1021880840255,
4.70238175978817));
#195002=CARTESIAN_POINT('Ctrl Pts',(-20.8480268211227,19.0987895664123,
4.70217548757971));
#195003=CARTESIAN_POINT('Ctrl Pts',(-20.8476550551931,19.0919920245619,
4.70176379849832));
#195004=CARTESIAN_POINT('Ctrl Pts',(-20.8474609357335,19.0885930391345,
4.70155838161796));
#195005=CARTESIAN_POINT('Ctrl Pts',(-20.8469736811945,19.0804082226764,
4.70106476398547));
#195006=CARTESIAN_POINT('Ctrl Pts',(-20.8466724833825,19.0756228649065,
4.70077701234596));
#195007=CARTESIAN_POINT('Ctrl Pts',(-20.8455076186839,19.0580673441033,
4.69972434795524));
#195008=CARTESIAN_POINT('Ctrl Pts',(-20.8445443839743,19.0453037649106,
4.69896480349769));
#195009=CARTESIAN_POINT('Ctrl Pts',(-20.8412948240264,19.0068907097402,
4.69669422891624));
#195010=CARTESIAN_POINT('Ctrl Pts',(-20.8386561526834,18.9812725967026,
4.69520057613638));
#195011=CARTESIAN_POINT('Ctrl Pts',(-20.8271568183861,18.8866107253501,
4.68973698366177));
#195012=CARTESIAN_POINT('Ctrl Pts',(-20.815359701632,18.8179642595826,4.68588409709238));
#195013=CARTESIAN_POINT('Ctrl Pts',(-20.7628523866104,18.5826167235474,
4.67268986147537));
#195014=CARTESIAN_POINT('Ctrl Pts',(-20.7053025210351,18.420385130281,4.6635643276233));
#195015=CARTESIAN_POINT('Ctrl Pts',(-20.6094430852125,18.2280002287463,
4.65129081970063));
#195016=CARTESIAN_POINT('Ctrl Pts',(-20.5888830986371,18.1897343057494,
4.64877505454473));
#195017=CARTESIAN_POINT('Ctrl Pts',(-20.5612889500311,18.1419621330024,
4.64552585314126));
#195018=CARTESIAN_POINT('Ctrl Pts',(-20.5553316401202,18.1318438869678,
4.64483133656453));
#195019=CARTESIAN_POINT('Ctrl Pts',(-20.545635240889,18.1156839603565,4.64371168324615));
#195020=CARTESIAN_POINT('Ctrl Pts',(-20.5419493182459,18.1096105441325,
4.64328848994679));
#195021=CARTESIAN_POINT('Ctrl Pts',(-20.5348872058423,18.0981050467459,
4.64248217973361));
#195022=CARTESIAN_POINT('Ctrl Pts',(-20.5315168278889,18.0926694776544,
4.64209927979589));
#195023=CARTESIAN_POINT('Ctrl Pts',(-20.5237892059008,18.0803319583397,
4.64122563817267));
#195024=CARTESIAN_POINT('Ctrl Pts',(-20.5194165919564,18.0734397984084,
4.64073433061718));
#195025=CARTESIAN_POINT('Ctrl Pts',(-20.5079762063604,18.055635798028,4.63945659847115));
#195026=CARTESIAN_POINT('Ctrl Pts',(-20.5008476596439,18.0447635935634,
4.63866791487524));
#195027=CARTESIAN_POINT('Ctrl Pts',(-20.4535528492585,17.9740601968294,
4.63348284501959));
#195028=CARTESIAN_POINT('Ctrl Pts',(-20.4104582071831,17.9162536842956,
4.62897579343002));
#195029=CARTESIAN_POINT('Ctrl Pts',(-20.2374623580639,17.7073494951758,
4.61164117641781));
#195030=CARTESIAN_POINT('Ctrl Pts',(-20.0894289020334,17.5726593379008,
4.59813842911275));
#195031=CARTESIAN_POINT('Ctrl Pts',(-19.9014491080653,17.4447759395971,
4.58356919259272));
#195032=CARTESIAN_POINT('Ctrl Pts',(-19.8778080894437,17.4293748818869,
4.58178006681209));
#195033=CARTESIAN_POINT('Ctrl Pts',(-19.8437610561343,17.4081519307837,
4.57927156501528));
#195034=CARTESIAN_POINT('Ctrl Pts',(-19.8336037186753,17.4019387964087,
4.5785316279267));
#195035=CARTESIAN_POINT('Ctrl Pts',(-19.8178770363495,17.3925003509142,
4.57739954164229));
#195036=CARTESIAN_POINT('Ctrl Pts',(-19.8123446702371,17.3892142886145,
4.57700385241569));
#195037=CARTESIAN_POINT('Ctrl Pts',(-19.8031433772348,17.383805592284,4.57635009554928));
#195038=CARTESIAN_POINT('Ctrl Pts',(-19.7994829476587,17.3816686867517,
4.57609115314194));
#195039=CARTESIAN_POINT('Ctrl Pts',(-19.7923782198309,17.37754960923,4.575590786715));
#195040=CARTESIAN_POINT('Ctrl Pts',(-19.7889347124578,17.375566115416,4.57534927944021));
#195041=CARTESIAN_POINT('Ctrl Pts',(-19.7824724983168,17.3718680111772,
4.57489797617566));
#195042=CARTESIAN_POINT('Ctrl Pts',(-19.7794551945294,17.3701511500241,
4.57468803970332));
#195043=CARTESIAN_POINT('Ctrl Pts',(-19.7724408688373,17.3661827714855,
4.57420179984742));
#195044=CARTESIAN_POINT('Ctrl Pts',(-19.7684407476192,17.3639368215274,
4.57392585599385));
#195045=CARTESIAN_POINT('Ctrl Pts',(-19.7561078677403,17.3570649041168,
4.57307912973231));
#195046=CARTESIAN_POINT('Ctrl Pts',(-19.7477510133827,17.3524821164191,
4.57251104198148));
#195047=CARTESIAN_POINT('Ctrl Pts',(-19.6351305199465,17.291708188119,4.56492711157822));
#195048=CARTESIAN_POINT('Ctrl Pts',(-19.5263450888224,17.2442985344387,
4.55841883662445));
#195049=CARTESIAN_POINT('Ctrl Pts',(-19.3106039756828,17.171104675059,4.54601545495623));
#195050=CARTESIAN_POINT('Ctrl Pts',(-19.2044919573254,17.144050190448,4.54012765391835));
#195051=CARTESIAN_POINT('Ctrl Pts',(-19.0424815618063,17.1158712547053,
4.53098398998122));
#195052=CARTESIAN_POINT('Ctrl Pts',(-18.9878490398172,17.1085525326042,
4.52787685894774));
#195053=CARTESIAN_POINT('Ctrl Pts',(-18.8988433881107,17.1001488801067,
4.5227334288636));
#195054=CARTESIAN_POINT('Ctrl Pts',(-18.8646190761696,17.0977550417999,
4.5207365058017));
#195055=CARTESIAN_POINT('Ctrl Pts',(-18.8195557280447,17.0957019023244,
4.51807607455091));
#195056=CARTESIAN_POINT('Ctrl Pts',(-18.8087549307922,17.0952926671215,
4.51743608981436));
#195057=CARTESIAN_POINT('Ctrl Pts',(-18.7910566771901,17.094757783409,4.51638340946749));
#195058=CARTESIAN_POINT('Ctrl Pts',(-18.7841608183004,17.0945831048043,
4.51597225498933));
#195059=CARTESIAN_POINT('Ctrl Pts',(-18.7708087734838,17.0943101773493,
4.51517418921256));
#195060=CARTESIAN_POINT('Ctrl Pts',(-18.7643527423884,17.094207756837,4.51478741325659));
#195061=CARTESIAN_POINT('Ctrl Pts',(-18.7494420108875,17.09403943587,4.51389201933557));
#195062=CARTESIAN_POINT('Ctrl Pts',(-18.7409872248408,17.0939946478029,
4.51338274517082));
#195063=CARTESIAN_POINT('Ctrl Pts',(-18.7182418348187,17.0940104149501,
4.51200837633005));
#195064=CARTESIAN_POINT('Ctrl Pts',(-18.7039519283694,17.0941650228108,
4.51114035318679));
#195065=CARTESIAN_POINT('Ctrl Pts',(-18.5727877356283,17.0969125175869,
4.50312970998661));
#195066=CARTESIAN_POINT('Ctrl Pts',(-18.4563334254439,17.1090369333371,
4.49568501739993));
#195067=CARTESIAN_POINT('Ctrl Pts',(-18.1814277000123,17.1609061046711,
4.47741112914737));
#195068=CARTESIAN_POINT('Ctrl Pts',(-18.0253895151496,17.2094774780682,
4.46644146029023));
#195069=CARTESIAN_POINT('Ctrl Pts',(-17.8469187509254,17.2885484035777,
4.45404010779418));
#195070=CARTESIAN_POINT('Ctrl Pts',(-17.8176749663243,17.3023140698814,
4.45201499635562));
#195071=CARTESIAN_POINT('Ctrl Pts',(-17.782289997379,17.3199713666781,4.44958327965227));
#195072=CARTESIAN_POINT('Ctrl Pts',(-17.775840377276,17.3232311153155,4.44914082387328));
#195073=CARTESIAN_POINT('Ctrl Pts',(-17.7657517733806,17.3283950926444,
4.44845009266478));
#195074=CARTESIAN_POINT('Ctrl Pts',(-17.7621014943149,17.33027695796,4.44820045284476));
#195075=CARTESIAN_POINT('Ctrl Pts',(-17.7552862699309,17.3338156201542,
4.44773492577405));
#195076=CARTESIAN_POINT('Ctrl Pts',(-17.7521200771149,17.3354697873334,
4.44751888414557));
#195077=CARTESIAN_POINT('Ctrl Pts',(-17.7448989481459,17.3392657405255,
4.44702667033214));
#195078=CARTESIAN_POINT('Ctrl Pts',(-17.7408467821932,17.3414126883889,
4.44675082879972));
#195079=CARTESIAN_POINT('Ctrl Pts',(-17.7284022734093,17.348058004763,4.44590472857384));
#195080=CARTESIAN_POINT('Ctrl Pts',(-17.7200331443874,17.352599911558,4.44533715876251));
#195081=CARTESIAN_POINT('Ctrl Pts',(-17.6079266222893,17.414422640176,4.43775007482204));
#195082=CARTESIAN_POINT('Ctrl Pts',(-17.509130518653,17.4802676844073,4.43123870275612));
#195083=CARTESIAN_POINT('Ctrl Pts',(-17.3307843951688,17.622092341876,4.41883304774966));
#195084=CARTESIAN_POINT('Ctrl Pts',(-17.2506152416133,17.6966650462839,
4.41294603043153));
#195085=CARTESIAN_POINT('Ctrl Pts',(-17.1392571530733,17.8176161842848,
4.40380418848833));
#195086=CARTESIAN_POINT('Ctrl Pts',(-17.1035454617429,17.8595783190234,
4.40069810176586));
#195087=CARTESIAN_POINT('Ctrl Pts',(-17.0483206513809,17.9298480467366,
4.39555624627508));
#195088=CARTESIAN_POINT('Ctrl Pts',(-17.0277883227301,17.9573227250749,
4.393559821887));
#195089=CARTESIAN_POINT('Ctrl Pts',(-17.0016757672682,17.9940946809114,
4.39089996085846));
#195090=CARTESIAN_POINT('Ctrl Pts',(-16.9954859929765,18.0029541218301,
4.39026003480146));
#195091=CARTESIAN_POINT('Ctrl Pts',(-16.9854572266273,18.0175450363167,
4.38920742638816));
#195092=CARTESIAN_POINT('Ctrl Pts',(-16.9815778835294,18.0232486351817,
4.38879628475046));
#195093=CARTESIAN_POINT('Ctrl Pts',(-16.9741212726445,18.0343277613249,
4.3879982263231));
#195094=CARTESIAN_POINT('Ctrl Pts',(-16.9705405834183,18.0397009020307,
4.38761144478309));
#195095=CARTESIAN_POINT('Ctrl Pts',(-16.9623278246113,18.0521478964474,
4.38671601232906));
#195096=CARTESIAN_POINT('Ctrl Pts',(-16.9577134656275,18.0592332529884,
4.38620670503767));
#195097=CARTESIAN_POINT('Ctrl Pts',(-16.9454138097052,18.0783691173359,
4.38483218883365));
#195098=CARTESIAN_POINT('Ctrl Pts',(-16.9378080003604,18.0904699641766,
4.38396405047665));
#195099=CARTESIAN_POINT('Ctrl Pts',(-16.8690460597599,18.2023694451796,
4.37594452549632));
#195100=CARTESIAN_POINT('Ctrl Pts',(-16.8161523942463,18.3069858895769,
4.36849028879542));
#195101=CARTESIAN_POINT('Ctrl Pts',(-16.7107926865835,18.5667929340149,
4.35017616402295));
#195102=CARTESIAN_POINT('Ctrl Pts',(-16.6671333362167,18.7247562947737,
4.3391746047566));
#195103=CARTESIAN_POINT('Ctrl Pts',(-16.637193347888,18.9175706191703,4.32678446692435));
#195104=CARTESIAN_POINT('Ctrl Pts',(-16.6330245216234,18.9490816365276,
4.32479368431312));
#195105=CARTESIAN_POINT('Ctrl Pts',(-16.6287844060638,18.9878229682364,
4.32239740568799));
#195106=CARTESIAN_POINT('Ctrl Pts',(-16.6280386384158,18.994973540069,4.32195725595343));
#195107=CARTESIAN_POINT('Ctrl Pts',(-16.6269249166321,19.0062064664921,
4.32126931948258));
#195108=CARTESIAN_POINT('Ctrl Pts',(-16.6265323752652,19.0102862494254,
4.32102018614093));
#195109=CARTESIAN_POINT('Ctrl Pts',(-16.6258197612817,19.0179252704006,
4.32055509481909));
#195110=CARTESIAN_POINT('Ctrl Pts',(-16.6254968559095,19.0214841386238,
4.3203389855196));
#195111=CARTESIAN_POINT('Ctrl Pts',(-16.6247790474197,19.0296243754028,
4.31984595633227));
#195112=CARTESIAN_POINT('Ctrl Pts',(-16.6243900591065,19.034206215606,4.31956937131007));
#195113=CARTESIAN_POINT('Ctrl Pts',(-16.6234119662117,19.0461901445694,
4.31884828388752));
#195114=CARTESIAN_POINT('Ctrl Pts',(-16.6228468659472,19.0535942025803,
4.31840509402368));
#195115=CARTESIAN_POINT('Ctrl Pts',(-16.6193611045964,19.1026666628772,
4.3154822002857));
#195116=CARTESIAN_POINT('Ctrl Pts',(-16.6176350585818,19.1444137639373,
4.31306467071894));
#195117=CARTESIAN_POINT('Ctrl Pts',(-16.6170489590419,19.1944164593618,
4.31022283046059));
#195118=CARTESIAN_POINT('Ctrl Pts',(-16.61700048749,19.2026459166037,4.30975686326737));
#195119=CARTESIAN_POINT('Ctrl Pts',(-16.6169984731698,19.2369080501551,
4.30782338691925));
#195120=CARTESIAN_POINT('Ctrl Pts',(-16.6174771214944,19.2629391384073,
4.30637003367368));
#195121=CARTESIAN_POINT('Ctrl Pts',(-16.6200726497615,19.3333768594573,
4.30246461686822));
#195122=CARTESIAN_POINT('Ctrl Pts',(-16.6231082557594,19.3777369073968,
4.30003426143808));
#195123=CARTESIAN_POINT('Ctrl Pts',(-16.6384343473003,19.5307628983407,
4.29166126775283));
#195124=CARTESIAN_POINT('Ctrl Pts',(-16.6577423292433,19.6385475593011,
4.2857737723225));
#195125=CARTESIAN_POINT('Ctrl Pts',(-16.7043541571101,19.8175921656384,
4.27548628601285));
#195126=CARTESIAN_POINT('Ctrl Pts',(-16.72733223724,19.889748149863,4.27119623087738));
#195127=CARTESIAN_POINT('Ctrl Pts',(-16.7608112661022,19.9781845935418,
4.26567538912572));
#195128=CARTESIAN_POINT('Ctrl Pts',(-16.7677366613975,19.9957639321345,
4.26456475847457));
#195129=CARTESIAN_POINT('Ctrl Pts',(-16.7781439846533,20.0211788047035,
4.26293885389868));
#195130=CARTESIAN_POINT('Ctrl Pts',(-16.7814397989613,20.0290899133859,
4.26242986571197));
#195131=CARTESIAN_POINT('Ctrl Pts',(-16.7873007725456,20.0429211157723,
4.26153483933823));
#195132=CARTESIAN_POINT('Ctrl Pts',(-16.7898451435989,20.0488499376076,
4.26114951237064));
#195133=CARTESIAN_POINT('Ctrl Pts',(-16.7948370813972,20.060336833812,4.26039966959961));
#195134=CARTESIAN_POINT('Ctrl Pts',(-16.7972815440673,20.065896194522,4.26003526295441));
#195135=CARTESIAN_POINT('Ctrl Pts',(-16.8031803317689,20.0791564633059,
4.2591624428008));
#195136=CARTESIAN_POINT('Ctrl Pts',(-16.8066568357113,20.0868473382104,
4.2586532710136));
#195137=CARTESIAN_POINT('Ctrl Pts',(-16.8193555616691,20.1144982713477,
4.25681189124235));
#195138=CARTESIAN_POINT('Ctrl Pts',(-16.8288423736915,20.1343346160819,
4.25547058551369));
#195139=CARTESIAN_POINT('Ctrl Pts',(-16.9218540721198,20.3212778320708,
4.24263112929833));
#195140=CARTESIAN_POINT('Ctrl Pts',(-17.0268314031326,20.4767554904814,
4.23032151974281));
#195141=CARTESIAN_POINT('Ctrl Pts',(-17.203480495964,20.6757509026055,4.21275586767703));
#195142=CARTESIAN_POINT('Ctrl Pts',(-17.2594556963321,20.732087093671,4.20754440657923));
#195143=CARTESIAN_POINT('Ctrl Pts',(-17.3450953158364,20.8090974298502,
4.2002039866135));
#195144=CARTESIAN_POINT('Ctrl Pts',(-17.372330752474,20.8323663465069,4.19795424391827));
#195145=CARTESIAN_POINT('Ctrl Pts',(-17.4059329352687,20.8596304682066,
4.19529214563405));
#195146=CARTESIAN_POINT('Ctrl Pts',(-17.4117454433443,20.8642959324707,
4.19483564366738));
#195147=CARTESIAN_POINT('Ctrl Pts',(-17.4208376849063,20.8715152845359,
4.19412790726711));
#195148=CARTESIAN_POINT('Ctrl Pts',(-17.4241004390102,20.8740903212888,
4.1938751980102));
#195149=CARTESIAN_POINT('Ctrl Pts',(-17.4301766274713,20.878856807584,4.19340695426395));
#195150=CARTESIAN_POINT('Ctrl Pts',(-17.4329879882371,20.8810507366181,
4.19319124704778));
#195151=CARTESIAN_POINT('Ctrl Pts',(-17.4393708098283,20.8860058622604,
4.19270362923973));
#195152=CARTESIAN_POINT('Ctrl Pts',(-17.4429455577205,20.8887627384671,
4.1924320252486));
#195153=CARTESIAN_POINT('Ctrl Pts',(-17.4535663338135,20.8968995270186,
4.19162938938989));
#195154=CARTESIAN_POINT('Ctrl Pts',(-17.4606374673259,20.9022467162709,
4.1911006083338));
#195155=CARTESIAN_POINT('Ctrl Pts',(-17.5135319948742,20.9417257381824,
4.1871849170608));
#195156=CARTESIAN_POINT('Ctrl Pts',(-17.5606911631499,20.9740375302445,
4.18391448520274));
#195157=CARTESIAN_POINT('Ctrl Pts',(-17.7373501869243,21.0848452268982,
4.17222289170266));
#195158=CARTESIAN_POINT('Ctrl Pts',(-17.8738598788654,21.1513018608102,
4.16420749353028));
#195159=CARTESIAN_POINT('Ctrl Pts',(-18.1035156055683,21.2340603346366,
4.15076204402042));
#195160=CARTESIAN_POINT('Ctrl Pts',(-18.1926939348683,21.2597236409817,
4.14555624900042));
#195161=CARTESIAN_POINT('Ctrl Pts',(-18.3038463138748,21.2839449340748,
4.13892976063124));
#195162=CARTESIAN_POINT('Ctrl Pts',(-18.324497247321,21.288123092583,4.13769322565967));
#195163=CARTESIAN_POINT('Ctrl Pts',(-18.3540092600314,21.2936368453675,
4.13591710654804));
#195164=CARTESIAN_POINT('Ctrl Pts',(-18.3628221935975,21.2952255694682,
4.1353855831559));
#195165=CARTESIAN_POINT('Ctrl Pts',(-18.3780651898459,21.2978737086659,
4.13446418950468));
#195166=CARTESIAN_POINT('Ctrl Pts',(-18.3844905993502,21.2989594446238,
4.13407516149355));
#195167=CARTESIAN_POINT('Ctrl Pts',(-18.3968182685827,21.3009840184618,
4.13332753124733));
#195168=CARTESIAN_POINT('Ctrl Pts',(-18.4027196999227,21.3019275642809,
4.13296908265181));
#195169=CARTESIAN_POINT('Ctrl Pts',(-18.4181096159665,21.3043213799239,
4.13203284768305));
#195170=CARTESIAN_POINT('Ctrl Pts',(-18.4276040300351,21.305732116337,4.13145381406636));
#195171=CARTESIAN_POINT('Ctrl Pts',(-18.4601866293815,21.3103471762095,
4.12946157190856));
#195172=CARTESIAN_POINT('Ctrl Pts',(-18.4833173229155,21.3132346337751,
4.12803841341041));
#195173=CARTESIAN_POINT('Ctrl Pts',(-18.6762836344439,21.3340931355481,
4.11608808533391));
#195174=CARTESIAN_POINT('Ctrl Pts',(-18.8476436772053,21.3318298100536,
4.10489906855872));
#195175=CARTESIAN_POINT('Ctrl Pts',(-19.1063745545575,21.2969505592224,
4.08764697788675));
#195176=CARTESIAN_POINT('Ctrl Pts',(-19.1950578905991,21.2791586405268,
4.08168383185548));
#195177=CARTESIAN_POINT('Ctrl Pts',(-19.3196740187697,21.2457405765133,
4.07344070081578));
#195178=CARTESIAN_POINT('Ctrl Pts',(-19.3567321701541,21.2347065868923,
4.07100780714257));
#195179=CARTESIAN_POINT('Ctrl Pts',(-19.4007094674453,21.2202898073772,
4.0681596518496));
#195180=CARTESIAN_POINT('Ctrl Pts',(-19.407936305669,21.2178774013286,4.06769289049096));
#195181=CARTESIAN_POINT('Ctrl Pts',(-19.4191195770003,21.214077068325,4.0669727539404));
#195182=CARTESIAN_POINT('Ctrl Pts',(-19.4230850900762,21.2127163424863,
4.0667178209751));
#195183=CARTESIAN_POINT('Ctrl Pts',(-19.4304131528273,21.2101774345724,
4.06624753536373));
#195184=CARTESIAN_POINT('Ctrl Pts',(-19.433776742609,21.2090025538389,4.06603199687738));
#195185=CARTESIAN_POINT('Ctrl Pts',(-19.4413507359171,21.2063355330595,
4.06554737376713));
#195186=CARTESIAN_POINT('Ctrl Pts',(-19.44555937988,21.2048385598734,4.06527857973651));
#195187=CARTESIAN_POINT('Ctrl Pts',(-19.4578987970621,21.2004055042796,
4.06449186908883));
#195188=CARTESIAN_POINT('Ctrl Pts',(-19.4660164742409,21.1974328873808,
4.06397607251001));
#195189=CARTESIAN_POINT('Ctrl Pts',(-19.5224621650846,21.1763700009335,
4.06040026662786));
#195190=CARTESIAN_POINT('Ctrl Pts',(-19.5701370130605,21.1565661524418,
4.05743505377173));
#195191=CARTESIAN_POINT('Ctrl Pts',(-19.636925934135,21.1259131308532,4.05329619516721));
#195192=CARTESIAN_POINT('Ctrl Pts',(-19.6566654427852,21.1164805346011,
4.05207491840168));
#195193=CARTESIAN_POINT('Ctrl Pts',(-19.7995547650047,21.0454591781868,
4.04322471149285));
#195194=CARTESIAN_POINT('Ctrl Pts',(-19.916583212246,20.9722912961926,4.03590134546389));
#195195=CARTESIAN_POINT('Ctrl Pts',(-20.0975673974847,20.832914122616,4.0233071191621));
#195196=CARTESIAN_POINT('Ctrl Pts',(-20.1658131725678,20.7729954462517,
4.01820661662544));
#195197=CARTESIAN_POINT('Ctrl Pts',(-20.2447378791476,20.6941702107017,
4.01170751222547));
#195198=CARTESIAN_POINT('Ctrl Pts',(-20.2592564945129,20.6792354694394,
4.01048489129421));
#195199=CARTESIAN_POINT('Ctrl Pts',(-20.279670357033,20.6576069275721,4.00872530717446));
#195200=CARTESIAN_POINT('Ctrl Pts',(-20.2857476193548,20.6510860313311,
4.00819619783071));
#195201=CARTESIAN_POINT('Ctrl Pts',(-20.2961911308814,20.6397372885967,
4.00727765435714));
#195202=CARTESIAN_POINT('Ctrl Pts',(-20.3005766609677,20.6349272920634,
4.00688904825375));
#195203=CARTESIAN_POINT('Ctrl Pts',(-20.3089521401547,20.6256556406509,
4.00614128713957));
#195204=CARTESIAN_POINT('Ctrl Pts',(-20.3129454924414,20.6211971337934,
4.00578228124705));
#195205=CARTESIAN_POINT('Ctrl Pts',(-20.323326263625,20.6095078159399,4.0048424946448));
#195206=CARTESIAN_POINT('Ctrl Pts',(-20.3296832005953,20.602250229833,4.00426044806461));
#195207=CARTESIAN_POINT('Ctrl Pts',(-20.3514219070606,20.577086598985,4.00224712433017));
#195208=CARTESIAN_POINT('Ctrl Pts',(-20.3665532241883,20.5589674034557,
4.00080561241734));
#195209=CARTESIAN_POINT('Ctrl Pts',(-20.4850678695611,20.4121273915577,
3.98918380176066));
#195210=CARTESIAN_POINT('Ctrl Pts',(-20.5733549462891,20.2719898213501,
3.97838997625524));
#195211=CARTESIAN_POINT('Ctrl Pts',(-20.6734505473955,20.0623223155182,
3.963036326288));
#195212=CARTESIAN_POINT('Ctrl Pts',(-20.6995188410847,20.0002690167383,
3.95859029255549));
#195213=CARTESIAN_POINT('Ctrl Pts',(-20.7225806759744,19.9371101122702,
3.95421657486109));
#195214=CARTESIAN_POINT('',(-20.8509992439641,19.2092108506511,4.48828862659254));
#195215=CARTESIAN_POINT('Ctrl Pts',(-20.7225806064494,19.9371103026767,
3.73234504707874));
#195216=CARTESIAN_POINT('Ctrl Pts',(-20.7168696304283,19.9527508136538,
3.73327499017389));
#195217=CARTESIAN_POINT('Ctrl Pts',(-20.7109725058956,19.9683284018271,
3.73420949014154));
#195218=CARTESIAN_POINT('Ctrl Pts',(-20.6832634653051,20.0389917889889,
3.7384902088931));
#195219=CARTESIAN_POINT('Ctrl Pts',(-20.6593330525292,20.0932075531427,
3.74189155812553));
#195220=CARTESIAN_POINT('Ctrl Pts',(-20.6277538445489,20.1573272320699,
3.7460905102994));
#195221=CARTESIAN_POINT('Ctrl Pts',(-20.622250176804,20.168261779382,3.74681289219443));
#195222=CARTESIAN_POINT('Ctrl Pts',(-20.6130255007591,20.1862000066534,
3.74800870193385));
#195223=CARTESIAN_POINT('Ctrl Pts',(-20.6093593733053,20.1932316955886,
3.7484801987666));
#195224=CARTESIAN_POINT('Ctrl Pts',(-20.6026761015929,20.2058764927002,
3.74933311093481));
#195225=CARTESIAN_POINT('Ctrl Pts',(-20.5996729429309,20.2114969150553,
3.74971402699587));
#195226=CARTESIAN_POINT('Ctrl Pts',(-20.5931997764901,20.2234809763269,
3.75053014623025));
#195227=CARTESIAN_POINT('Ctrl Pts',(-20.5897223786286,20.2298405114377,
3.7509656096224));
#195228=CARTESIAN_POINT('Ctrl Pts',(-20.5802117563529,20.2470235020649,
3.75214872340126));
#195229=CARTESIAN_POINT('Ctrl Pts',(-20.5741161202903,20.2578119218562,
3.75289860566175));
#195230=CARTESIAN_POINT('Ctrl Pts',(-20.5423238334514,20.3129439982901,
3.7567676853936));
#195231=CARTESIAN_POINT('Ctrl Pts',(-20.5151195681332,20.3563942699004,
3.75994128189931));
#195232=CARTESIAN_POINT('Ctrl Pts',(-20.3905638624033,20.540150084319,3.77392327858955));
#195233=CARTESIAN_POINT('Ctrl Pts',(-20.278021974646,20.6693632296009,3.78529518480088));
#195234=CARTESIAN_POINT('Ctrl Pts',(-20.0828463791118,20.8452499981519,
3.80257347817695));
#195235=CARTESIAN_POINT('Ctrl Pts',(-20.0105227441864,20.9023465867342,
3.80854955411206));
#195236=CARTESIAN_POINT('Ctrl Pts',(-19.9267413411507,20.960042758568,3.81483435935799));
#195237=CARTESIAN_POINT('Ctrl Pts',(-19.9187407994087,20.9654719218458,
3.81542839819196));
#195238=CARTESIAN_POINT('Ctrl Pts',(-19.9068673040276,20.9734110131545,
3.81630067326625));
#195239=CARTESIAN_POINT('Ctrl Pts',(-19.9030230193468,20.9759633065063,
3.81658165812261));
#195240=CARTESIAN_POINT('Ctrl Pts',(-19.8961854756308,20.9804707405698,
3.81707884488073));
#195241=CARTESIAN_POINT('Ctrl Pts',(-19.8931955816986,20.9824308864719,
3.81729537992134));
#195242=CARTESIAN_POINT('Ctrl Pts',(-19.8867759724377,20.9866163074762,
3.81775842541092));
#195243=CARTESIAN_POINT('Ctrl Pts',(-19.8833447821085,20.9888392184039,
3.81800477846252));
#195244=CARTESIAN_POINT('Ctrl Pts',(-19.8739014914335,20.9949183290227,
3.81867973056067));
#195245=CARTESIAN_POINT('Ctrl Pts',(-19.8678762176468,20.9987541053402,
3.81910699066484));
#195246=CARTESIAN_POINT('Ctrl Pts',(-19.835494536006,21.019139185873,3.82138575513574));
#195247=CARTESIAN_POINT('Ctrl Pts',(-19.8087935372755,21.0351372239326,
3.82320308113566));
#195248=CARTESIAN_POINT('Ctrl Pts',(-19.6393305023987,21.1316583053444,
3.83441829111504));
#195249=CARTESIAN_POINT('Ctrl Pts',(-19.4879597995627,21.1959706914068,
3.84307899541137));
#195250=CARTESIAN_POINT('Ctrl Pts',(-19.2182120936925,21.2752106745866,
3.85846837068923));
#195251=CARTESIAN_POINT('Ctrl Pts',(-19.1032202626038,21.2988453394168,
3.86501042879958));
#195252=CARTESIAN_POINT('Ctrl Pts',(-18.972679902309,21.3145506285162,3.87271301899665));
#195253=CARTESIAN_POINT('Ctrl Pts',(-18.9584707434067,21.3161142992548,
3.87355481392854));
#195254=CARTESIAN_POINT('Ctrl Pts',(-18.9358327579793,21.3183737314754,
3.8749017672507));
#195255=CARTESIAN_POINT('Ctrl Pts',(-18.9274135621793,21.3191631097016,
3.87540398185882));
#195256=CARTESIAN_POINT('Ctrl Pts',(-18.9125575894412,21.3204662549907,
3.87629249215949));
#195257=CARTESIAN_POINT('Ctrl Pts',(-18.9061227318743,21.3210010562646,
3.8766781213542));
#195258=CARTESIAN_POINT('Ctrl Pts',(-18.892809139549,21.3220462415804,3.87747761624303));
#195259=CARTESIAN_POINT('Ctrl Pts',(-18.8859301633169,21.3225524621988,
3.87789160805452));
#195260=CARTESIAN_POINT('Ctrl Pts',(-18.8682679925928,21.3237654584227,
3.87895692664623));
#195261=CARTESIAN_POINT('Ctrl Pts',(-18.8574817358048,21.3244232965217,
3.87960978186614));
#195262=CARTESIAN_POINT('Ctrl Pts',(-18.8124546889602,21.3268235565145,
3.882344865898));
#195263=CARTESIAN_POINT('Ctrl Pts',(-18.7781807188865,21.3278165505495,
3.88445040522089));
#195264=CARTESIAN_POINT('Ctrl Pts',(-18.6888393957829,21.3282343219379,
3.89000362367824));
#195265=CARTESIAN_POINT('Ctrl Pts',(-18.6337945662457,21.3263436378429,
3.89348966655988));
#195266=CARTESIAN_POINT('Ctrl Pts',(-18.4698250632734,21.3142973777107,
3.90405719943152));
#195267=CARTESIAN_POINT('Ctrl Pts',(-18.3615528452754,21.2978464021971,
3.91128708690311));
#195268=CARTESIAN_POINT('Ctrl Pts',(-18.2114890425629,21.2629919115816,
3.92146384158483));
#195269=CARTESIAN_POINT('Ctrl Pts',(-18.1682631169347,21.2514976013884,
3.92441233777086));
#195270=CARTESIAN_POINT('Ctrl Pts',(-18.1012763192632,21.2313924980513,
3.92898260396063));
#195271=CARTESIAN_POINT('Ctrl Pts',(-18.0772506166834,21.2237109630246,
3.93062193163042));
#195272=CARTESIAN_POINT('Ctrl Pts',(-18.0061380222753,21.1995657388441,
3.9354643089776));
#195273=CARTESIAN_POINT('Ctrl Pts',(-17.9594859446093,21.1818641761618,
3.93862832067649));
#195274=CARTESIAN_POINT('Ctrl Pts',(-17.9062948955802,21.1595005349747,
3.94218673066462));
#195275=CARTESIAN_POINT('Ctrl Pts',(-17.8991074104856,21.1564316855042,
3.9426665007003));
#195276=CARTESIAN_POINT('Ctrl Pts',(-17.8876576180704,21.1514678114357,
3.9434288893544));
#195277=CARTESIAN_POINT('Ctrl Pts',(-17.883384373156,21.1495984140603,3.9437130015385));
#195278=CARTESIAN_POINT('Ctrl Pts',(-17.8758325585335,21.1462649777586,
3.94421429758045));
#195279=CARTESIAN_POINT('Ctrl Pts',(-17.8725514922228,21.1448067020571,
3.94443182916393));
#195280=CARTESIAN_POINT('Ctrl Pts',(-17.8656111889867,21.1417009029133,
3.94489138146119));
#195281=CARTESIAN_POINT('Ctrl Pts',(-17.8619529290507,21.1400513239073,
3.94513327373414));
#195282=CARTESIAN_POINT('Ctrl Pts',(-17.8521061852617,21.1355775049156,
3.94578350412289));
#195283=CARTESIAN_POINT('Ctrl Pts',(-17.8459265258999,21.1327337953971,
3.9461906622334));
#195284=CARTESIAN_POINT('Ctrl Pts',(-17.8155066540928,21.1185573343534,
3.94819091762249));
#195285=CARTESIAN_POINT('Ctrl Pts',(-17.7914679162794,21.1067949341273,
3.94975897206591));
#195286=CARTESIAN_POINT('Ctrl Pts',(-17.7228432581424,21.0715880656409,
3.95421700488871));
#195287=CARTESIAN_POINT('Ctrl Pts',(-17.6788607918092,21.0470032229055,
3.95705157878362));
#195288=CARTESIAN_POINT('Ctrl Pts',(-17.5228550937659,20.9523410686637,
3.96717097501148));
#195289=CARTESIAN_POINT('Ctrl Pts',(-17.4165757480954,20.8733887883335,
3.97420842372241));
#195290=CARTESIAN_POINT('Ctrl Pts',(-17.2410517516806,20.715526950815,3.98719497351883));
#195291=CARTESIAN_POINT('Ctrl Pts',(-17.1689926773416,20.6404208108032,
3.99303519302854));
#195292=CARTESIAN_POINT('Ctrl Pts',(-17.0937853362103,20.5495000894048,
3.9999498214986));
#195293=CARTESIAN_POINT('Ctrl Pts',(-17.0849332246235,20.5385787693355,
4.00077786993149));
#195294=CARTESIAN_POINT('Ctrl Pts',(-17.0709745739133,20.5210022060422,
4.00210692585956));
#195295=CARTESIAN_POINT('Ctrl Pts',(-17.065797586662,20.5144032578948,4.00260511211224));
#195296=CARTESIAN_POINT('Ctrl Pts',(-17.0567115108498,20.502678704127,4.00348894146171));
#195297=CARTESIAN_POINT('Ctrl Pts',(-17.0527863408113,20.4975656536958,
4.0038739406019));
#195298=CARTESIAN_POINT('Ctrl Pts',(-17.0446920832965,20.4869215242743,
4.00467455336182));
#195299=CARTESIAN_POINT('Ctrl Pts',(-17.0405266713653,20.4813877585102,
4.00509030507787));
#195300=CARTESIAN_POINT('Ctrl Pts',(-17.0298541693055,20.4670635339918,
4.00616531218814));
#195301=CARTESIAN_POINT('Ctrl Pts',(-17.02338796867,20.4582429935407,4.00682615001767));
#195302=CARTESIAN_POINT('Ctrl Pts',(-16.9962604088946,20.4206305111364,
4.00963964665945));
#195303=CARTESIAN_POINT('Ctrl Pts',(-16.976256356435,20.3913736294851,4.01181731999833));
#195304=CARTESIAN_POINT('Ctrl Pts',(-16.9256711461044,20.3132511307669,
4.01760782934577));
#195305=CARTESIAN_POINT('Ctrl Pts',(-16.8963365321344,20.2636171418002,
4.02126324208149));
#195306=CARTESIAN_POINT('Ctrl Pts',(-16.7931988145228,20.0716275062087,
4.03529985020796));
#195307=CARTESIAN_POINT('Ctrl Pts',(-16.7336272484179,19.9222597648831,
4.04606240769764));
#195308=CARTESIAN_POINT('Ctrl Pts',(-16.6877273811675,19.7538272705526,
4.05741698812309));
#195309=CARTESIAN_POINT('Ctrl Pts',(-16.6841109151314,19.7400064554014,
4.05834277012739));
#195310=CARTESIAN_POINT('Ctrl Pts',(-16.6786274231437,19.7181494897221,
4.05979653150733));
#195311=CARTESIAN_POINT('Ctrl Pts',(-16.6766670337921,19.7101373597414,
4.06032726254465));
#195312=CARTESIAN_POINT('Ctrl Pts',(-16.6647681487689,19.6602451900943,
4.06361787058717));
#195313=CARTESIAN_POINT('Ctrl Pts',(-16.6560612270731,19.6180782877685,
4.06633659837874));
#195314=CARTESIAN_POINT('Ctrl Pts',(-16.6473550468378,19.568292545095,4.06945132282921));
#195315=CARTESIAN_POINT('Ctrl Pts',(-16.6461037192063,19.5609060556804,
4.06991099376607));
#195316=CARTESIAN_POINT('Ctrl Pts',(-16.6441444281326,19.5489556422237,
4.07065056052939));
#195317=CARTESIAN_POINT('Ctrl Pts',(-16.6434121550079,19.5443958468252,
4.07093178094086));
#195318=CARTESIAN_POINT('Ctrl Pts',(-16.6421394154587,19.5363015204073,
4.07142922795462));
#195319=CARTESIAN_POINT('Ctrl Pts',(-16.641592977027,19.532767983536,4.07164578900032));
#195320=CARTESIAN_POINT('Ctrl Pts',(-16.6404412830981,19.5251935600743,
4.0721087168901));
#195321=CARTESIAN_POINT('Ctrl Pts',(-16.6398387745129,19.5211523119757,
4.07235492724245));
#195322=CARTESIAN_POINT('Ctrl Pts',(-16.6382167729572,19.5100527112808,
4.07302908587159));
#195323=CARTESIAN_POINT('Ctrl Pts',(-16.6372212292934,19.5029908369928,
4.07345570044128));
#195324=CARTESIAN_POINT('Ctrl Pts',(-16.6320932341326,19.4652362241726,
4.07572483700404));
#195325=CARTESIAN_POINT('Ctrl Pts',(-16.6285987401311,19.4344588844199,
4.0775335216847));
#195326=CARTESIAN_POINT('Ctrl Pts',(-16.6200627582494,19.3410300248442,
4.08292964150221));
#195327=CARTESIAN_POINT('Ctrl Pts',(-16.6171340551401,19.2782175275517,
4.08642992354793));
#195328=CARTESIAN_POINT('Ctrl Pts',(-16.616953707009,19.1907231919099,4.09123805107953));
#195329=CARTESIAN_POINT('Ctrl Pts',(-16.6173331192014,19.1660833855326,
4.09258457032675));
#195330=CARTESIAN_POINT('Ctrl Pts',(-16.624174195859,18.9579468847463,4.10393234758351));
#195331=CARTESIAN_POINT('Ctrl Pts',(-16.6540502841451,18.7760243720731,
4.11376258135185));
#195332=CARTESIAN_POINT('Ctrl Pts',(-16.7134517158726,18.578883608284,4.12573510593473));
#195333=CARTESIAN_POINT('Ctrl Pts',(-16.7202236136068,18.5576309534037,
4.12704244263184));
#195334=CARTESIAN_POINT('Ctrl Pts',(-16.7300347845924,18.5284426846403,
4.12886257430851));
#195335=CARTESIAN_POINT('Ctrl Pts',(-16.7327880585426,18.5204119639808,
4.12936595358267));
#195336=CARTESIAN_POINT('Ctrl Pts',(-16.7375979334902,18.5066529052532,
4.13023295115586));
#195337=CARTESIAN_POINT('Ctrl Pts',(-16.7396310843441,18.5009164358201,
4.13059578915481));
#195338=CARTESIAN_POINT('Ctrl Pts',(-16.7438681335245,18.4891234928006,
4.13134455932915));
#195339=CARTESIAN_POINT('Ctrl Pts',(-16.7460750074265,18.4830681624735,
4.13173058748616));
#195340=CARTESIAN_POINT('Ctrl Pts',(-16.7512655468315,18.4690257528709,
4.13262945798287));
#195341=CARTESIAN_POINT('Ctrl Pts',(-16.7542698664453,18.4610464746681,
4.13314298672208));
#195342=CARTESIAN_POINT('Ctrl Pts',(-16.7640008798335,18.4356675152782,
4.13478527875509));
#195343=CARTESIAN_POINT('Ctrl Pts',(-16.7709092494871,18.418338870885,4.13592012105316));
#195344=CARTESIAN_POINT('Ctrl Pts',(-16.8394972472511,18.2526941040955,
4.14690127404881));
#195345=CARTESIAN_POINT('Ctrl Pts',(-16.9176283329592,18.1117885085386,
4.15733620684613));
#195346=CARTESIAN_POINT('Ctrl Pts',(-17.0889479800298,17.8717711474586,
4.17681149319563));
#195347=CARTESIAN_POINT('Ctrl Pts',(-17.1772154353026,17.7701120455588,
4.18573912392085));
#195348=CARTESIAN_POINT('Ctrl Pts',(-17.2858831507387,17.6666903436825,
4.19509723160919));
#195349=CARTESIAN_POINT('Ctrl Pts',(-17.2973582224274,17.6560095949428,
4.19606709460667));
#195350=CARTESIAN_POINT('Ctrl Pts',(-17.3132315918932,17.641560726787,4.19738253965967));
#195351=CARTESIAN_POINT('Ctrl Pts',(-17.317527949004,17.6376820307599,4.19773600580456));
#195352=CARTESIAN_POINT('Ctrl Pts',(-17.3243811705881,17.6315458574981,
4.1982956677512));
#195353=CARTESIAN_POINT('Ctrl Pts',(-17.3269276389225,17.62927688783,4.19850271715049));
#195354=CARTESIAN_POINT('Ctrl Pts',(-17.3321988144442,17.6246029362627,
4.19892942087962));
#195355=CARTESIAN_POINT('Ctrl Pts',(-17.3349242327085,17.6221988150846,
4.19914900608805));
#195356=CARTESIAN_POINT('Ctrl Pts',(-17.3414341307431,17.6164861027618,
4.19967106828158));
#195357=CARTESIAN_POINT('Ctrl Pts',(-17.3452242593567,17.6131839241978,
4.19997306816115));
#195358=CARTESIAN_POINT('Ctrl Pts',(-17.3580511065571,17.6020885553827,
4.20098870327018));
#195359=CARTESIAN_POINT('Ctrl Pts',(-17.3671421337033,17.594358115691,4.20169785130045));
#195360=CARTESIAN_POINT('Ctrl Pts',(-17.4723890985755,17.5063852014455,
4.20979223754029));
#195361=CARTESIAN_POINT('Ctrl Pts',(-17.5754323550403,17.434738861008,4.21662725626206));
#195362=CARTESIAN_POINT('Ctrl Pts',(-17.8297782888984,17.2894984116068,
4.23254690378475));
#195363=CARTESIAN_POINT('Ctrl Pts',(-17.9846747828019,17.2239695446759,
4.24159473270096));
#195364=CARTESIAN_POINT('Ctrl Pts',(-18.1682311459902,17.1708661460297,
4.25269286268768));
#195365=CARTESIAN_POINT('Ctrl Pts',(-18.1908972254461,17.1647155990138,
4.25406828399201));
#195366=CARTESIAN_POINT('Ctrl Pts',(-18.2229927763016,17.1565771339279,
4.25602478122169));
#195367=CARTESIAN_POINT('Ctrl Pts',(-18.2323411768619,17.1542744189303,
4.25659569576602));
#195368=CARTESIAN_POINT('Ctrl Pts',(-18.2475226003015,17.1506445644508,
4.25752465905837));
#195369=CARTESIAN_POINT('Ctrl Pts',(-18.253346179477,17.1492782232074,4.25788144119941));
#195370=CARTESIAN_POINT('Ctrl Pts',(-18.2655216449632,17.146475977675,4.25862830898798));
#195371=CARTESIAN_POINT('Ctrl Pts',(-18.2718745141716,17.1450446660752,
4.2590185379482));
#195372=CARTESIAN_POINT('Ctrl Pts',(-18.286954905512,17.1417200679604,4.25994616334838));
#195373=CARTESIAN_POINT('Ctrl Pts',(-18.2956879512573,17.139852661505,4.26048438323833));
#195374=CARTESIAN_POINT('Ctrl Pts',(-18.32492261612,17.1337945286948,4.26228971333829));
#195375=CARTESIAN_POINT('Ctrl Pts',(-18.345474008329,17.1298526288414,4.2635647278182));
#195376=CARTESIAN_POINT('Ctrl Pts',(-18.4562178954664,17.1103086832154,
4.2704690663485));
#195377=CARTESIAN_POINT('Ctrl Pts',(-18.5472809602832,17.1002657380717,
4.2762725078705));
#195378=CARTESIAN_POINT('Ctrl Pts',(-18.7837439420155,17.0896100163733,
4.29162498583937));
#195379=CARTESIAN_POINT('Ctrl Pts',(-18.9290658749683,17.0980126758185,
4.30135479403314));
#195380=CARTESIAN_POINT('Ctrl Pts',(-19.0865430842553,17.1235114955406,
4.31173183814653));
#195381=CARTESIAN_POINT('Ctrl Pts',(-19.100683774883,17.125948944085,4.31266180418919));
#195382=CARTESIAN_POINT('Ctrl Pts',(-19.120066363348,17.1294932289692,4.31393308955556));
#195383=CARTESIAN_POINT('Ctrl Pts',(-19.125330267095,17.1304764366524,4.31427799662429));
#195384=CARTESIAN_POINT('Ctrl Pts',(-19.1756092459514,17.1400652637452,
4.31756877777429));
#195385=CARTESIAN_POINT('Ctrl Pts',(-19.2203412406334,17.1501112850594,
4.32046871052137));
#195386=CARTESIAN_POINT('Ctrl Pts',(-19.272101273721,17.1635151450424,4.32376474025844));
#195387=CARTESIAN_POINT('Ctrl Pts',(-19.2794770511915,17.1654677947515,
4.32423299237287));
#195388=CARTESIAN_POINT('Ctrl Pts',(-19.2912920776637,17.1686641337814,
4.32498059324628));
#195389=CARTESIAN_POINT('Ctrl Pts',(-19.2957380229532,17.1698825009898,
4.32526134776177));
#195390=CARTESIAN_POINT('Ctrl Pts',(-19.3036328512683,17.172073749403,4.32575884524867));
#195391=CARTESIAN_POINT('Ctrl Pts',(-19.307083282901,17.1730408757304,4.32597591777067));
#195392=CARTESIAN_POINT('Ctrl Pts',(-19.314422457802,17.1751180966599,4.32643686173727));
#195393=CARTESIAN_POINT('Ctrl Pts',(-19.3183104714978,17.1762305714414,
4.32668059263369));
#195394=CARTESIAN_POINT('Ctrl Pts',(-19.3288642272749,17.1792830546387,
4.32734099424625));
#195395=CARTESIAN_POINT('Ctrl Pts',(-19.3355237206898,17.1812447409963,
4.32775642060591));
#195396=CARTESIAN_POINT('Ctrl Pts',(-19.3694403074562,17.1914171295474,
4.32986614367105));
#195397=CARTESIAN_POINT('Ctrl Pts',(-19.3965408674416,17.200144676105,4.33153198673144));
#195398=CARTESIAN_POINT('Ctrl Pts',(-19.4756898391065,17.2274080625796,
4.33636077150797));
#195399=CARTESIAN_POINT('Ctrl Pts',(-19.5272005985897,17.2474383252249,
4.33945668235915));
#195400=CARTESIAN_POINT('Ctrl Pts',(-19.7259159502871,17.3338081697218,
4.35142543963522));
#195401=CARTESIAN_POINT('Ctrl Pts',(-19.8661127017717,17.4148737723795,
4.35996839628424));
#195402=CARTESIAN_POINT('Ctrl Pts',(-20.0519479649809,17.5528074995047,
4.37292802299029));
#195403=CARTESIAN_POINT('Ctrl Pts',(-20.1060490035588,17.5972871168664,
4.37692581698455));
#195404=CARTESIAN_POINT('Ctrl Pts',(-20.1673786866644,17.653026786268,4.38179011641081));
#195405=CARTESIAN_POINT('Ctrl Pts',(-20.1768336405713,17.6617788831947,
4.38254989036287));
#195406=CARTESIAN_POINT('Ctrl Pts',(-20.1921211863307,17.6761913311958,
4.38379489809854));
#195407=CARTESIAN_POINT('Ctrl Pts',(-20.1980021950148,17.6818000084878,
4.38427791398657));
#195408=CARTESIAN_POINT('Ctrl Pts',(-20.2084506497061,17.6918801445827,
4.38514344968623));
#195409=CARTESIAN_POINT('Ctrl Pts',(-20.2130304362591,17.6963387108741,
4.38552540553394));
#195410=CARTESIAN_POINT('Ctrl Pts',(-20.2218493349009,17.7050023212138,
4.38626593916208));
#195411=CARTESIAN_POINT('Ctrl Pts',(-20.2260909903834,17.7092046986508,
4.3866243976981));
#195412=CARTESIAN_POINT('Ctrl Pts',(-20.2374511255913,17.7205552736815,
4.38759063219959));
#195413=CARTESIAN_POINT('Ctrl Pts',(-20.2445363167496,17.7277364362605,
4.38819987051008));
#195414=CARTESIAN_POINT('Ctrl Pts',(-20.2725837053326,17.7565731190455,
4.39063837078836));
#195415=CARTESIAN_POINT('Ctrl Pts',(-20.2931329091294,17.7786237243496,
4.39248540385731));
#195416=CARTESIAN_POINT('Ctrl Pts',(-20.344199497341,17.8358226776798,4.39723505139397));
#195417=CARTESIAN_POINT('Ctrl Pts',(-20.3740400884609,17.8715511997458,
4.4001639251692));
#195418=CARTESIAN_POINT('Ctrl Pts',(-20.4508340277919,17.9699143125699,
4.40812607392659));
#195419=CARTESIAN_POINT('Ctrl Pts',(-20.4955297900635,18.0342146175184,
4.41322914731125));
#195420=CARTESIAN_POINT('Ctrl Pts',(-20.6177143447865,18.2326044191612,
4.42857136871366));
#195421=CARTESIAN_POINT('Ctrl Pts',(-20.6841792885624,18.3728803655174,
4.43893737344926));
#195422=CARTESIAN_POINT('Ctrl Pts',(-20.7397311164905,18.5335318573357,
4.44953435653013));
#195423=CARTESIAN_POINT('Ctrl Pts',(-20.7445474342756,18.5479619611808,
4.4504750949548));
#195424=CARTESIAN_POINT('Ctrl Pts',(-20.7509595400674,18.5678857772099,
4.45175754668922));
#195425=CARTESIAN_POINT('Ctrl Pts',(-20.7526891017257,18.5733355097367,
4.45210665204186));
#195426=CARTESIAN_POINT('Ctrl Pts',(-20.7554109991224,18.5820340937847,
4.45266112297374));
#195427=CARTESIAN_POINT('Ctrl Pts',(-20.7564176160349,18.5852783963428,
4.45286731466029));
#195428=CARTESIAN_POINT('Ctrl Pts',(-20.7584877194804,18.5920074733691,
4.4532936996337));
#195429=CARTESIAN_POINT('Ctrl Pts',(-20.7595500202379,18.5954925751611,
4.45351381769216));
#195430=CARTESIAN_POINT('Ctrl Pts',(-20.7620715715693,18.6038422824012,
4.45403950978165));
#195431=CARTESIAN_POINT('Ctrl Pts',(-20.7635223357588,18.6087094693374,
4.45434458876453));
#195432=CARTESIAN_POINT('Ctrl Pts',(-20.7684097856681,18.6253246229376,
4.45538156887731));
#195433=CARTESIAN_POINT('Ctrl Pts',(-20.7717621679711,18.6370974072122,
4.45610872234565));
#195434=CARTESIAN_POINT('Ctrl Pts',(-20.7901103991915,18.703720595444,4.46018435262102));
#195435=CARTESIAN_POINT('Ctrl Pts',(-20.8029949398621,18.7591333616955,
4.46342419049857));
#195436=CARTESIAN_POINT('Ctrl Pts',(-20.8383771231678,18.9449475174164,
4.47399382749415));
#195437=CARTESIAN_POINT('Ctrl Pts',(-20.8508874458946,19.0769265174022,
4.48104241160473));
#195438=CARTESIAN_POINT('Ctrl Pts',(-20.8509992439641,19.2092108506511,
4.48828862659254));
#195439=CARTESIAN_POINT('Ctrl Pts',(-20.8509992455944,19.2092127807703,
4.48828873231979));
#195440=CARTESIAN_POINT('Ctrl Pts',(-20.8510695258653,19.2924612585343,
4.49284888304316));
#195441=CARTESIAN_POINT('Ctrl Pts',(-20.8462293851984,19.3756367542194,
4.49747294574716));
#195442=CARTESIAN_POINT('Ctrl Pts',(-20.8325134256674,19.4922434801573,
4.50419755350081));
#195443=CARTESIAN_POINT('Ctrl Pts',(-20.8277010378865,19.526075018031,4.50617710565744));
#195444=CARTESIAN_POINT('Ctrl Pts',(-20.8203843855559,19.5698790278976,
4.50878348017379));
#195445=CARTESIAN_POINT('Ctrl Pts',(-20.8186232139868,19.5799715587436,
4.50938699187165));
#195446=CARTESIAN_POINT('Ctrl Pts',(-20.8155220145444,19.5970118712236,
4.51041121137972));
#195447=CARTESIAN_POINT('Ctrl Pts',(-20.8142202735552,19.6039665041733,
4.51083070588023));
#195448=CARTESIAN_POINT('Ctrl Pts',(-20.811575518071,19.6177147934122,4.51166297853968));
#195449=CARTESIAN_POINT('Ctrl Pts',(-20.8102339834277,19.6245086465562,
4.5120757049779));
#195450=CARTESIAN_POINT('Ctrl Pts',(-20.8075793183357,19.6376138382503,
4.51287469799734));
#195451=CARTESIAN_POINT('Ctrl Pts',(-20.8062706448965,19.6439260090253,
4.51326081796372));
#195452=CARTESIAN_POINT('Ctrl Pts',(-20.8031923800986,19.6584397055503,
4.51415162616798));
#195453=CARTESIAN_POINT('Ctrl Pts',(-20.8014028291732,19.6666368452202,
4.51465694945044));
#195454=CARTESIAN_POINT('Ctrl Pts',(-20.7964823801326,19.6885493087667,
4.51601378251425));
#195455=CARTESIAN_POINT('Ctrl Pts',(-20.7932634574221,19.7022442453515,
4.51686810563248));
#195456=CARTESIAN_POINT('Ctrl Pts',(-20.7715055147565,19.7908396492252,
4.52243687703536));
#195457=CARTESIAN_POINT('Ctrl Pts',(-20.7490266050673,19.8646832986012,
4.52727684458111));
#195458=CARTESIAN_POINT('Ctrl Pts',(-20.7225805792317,19.9371103772171,
4.53222349041431));
#195459=CARTESIAN_POINT('Origin',(-18.734,19.211,0.));
#195460=CARTESIAN_POINT('',(-20.722580628988,19.937110240951,5.55626853452768));
#195461=CARTESIAN_POINT('',(-20.7225805912209,19.9371103443827,5.33540100209137));
#195462=CARTESIAN_POINT('',(-20.7225806064498,19.9371103026755,0.));
#195463=CARTESIAN_POINT('Ctrl Pts',(-20.722580628988,19.937110240951,5.55626853452768));
#195464=CARTESIAN_POINT('Ctrl Pts',(-20.7320991031241,19.9110422250807,
5.55474537328154));
#195465=CARTESIAN_POINT('Ctrl Pts',(-20.7411068404243,19.8847819946634,
5.55321404310531));
#195466=CARTESIAN_POINT('Ctrl Pts',(-20.7754133503966,19.777963845185,5.54697990101072));
#195467=CARTESIAN_POINT('Ctrl Pts',(-20.7963949671106,19.6961196087105,
5.54218749179229));
#195468=CARTESIAN_POINT('Ctrl Pts',(-20.8151326623951,19.5993009538407,
5.5363985457184));
#195469=CARTESIAN_POINT('Ctrl Pts',(-20.8176912853412,19.5853279336306,
5.53556033389131));
#195470=CARTESIAN_POINT('Ctrl Pts',(-20.8214097407618,19.563800185921,5.53426431737361));
#195471=CARTESIAN_POINT('Ctrl Pts',(-20.8226696394578,19.5562629894375,
5.53380969628319));
#195472=CARTESIAN_POINT('Ctrl Pts',(-20.8248931359631,19.5425034518133,
5.53297812002155));
#195473=CARTESIAN_POINT('Ctrl Pts',(-20.8258698385693,19.5362832945917,
5.53260158575233));
#195474=CARTESIAN_POINT('Ctrl Pts',(-20.8279419771641,19.5226914148005,
5.5317774361913));
#195475=CARTESIAN_POINT('Ctrl Pts',(-20.829026260802,19.515318100229,5.53132947256093));
#195476=CARTESIAN_POINT('Ctrl Pts',(-20.8318905543936,19.495099272149,5.53009860290783));
#195477=CARTESIAN_POINT('Ctrl Pts',(-20.8335914776936,19.4822430454582,
5.52931320841856));
#195478=CARTESIAN_POINT('Ctrl Pts',(-20.8416314806073,19.4168589028857,
5.52530436524589));
#195479=CARTESIAN_POINT('Ctrl Pts',(-20.8461174158795,19.3641260456246,
5.52202308694846));
#195480=CARTESIAN_POINT('Ctrl Pts',(-20.8502336389503,19.2773299092953,
5.51653982374483));
#195481=CARTESIAN_POINT('Ctrl Pts',(-20.8510257892788,19.2433434161714,
5.51437226626602));
#195482=CARTESIAN_POINT('Ctrl Pts',(-20.8508977921059,19.0787312499579,
5.50378105246286));
#195483=CARTESIAN_POINT('Ctrl Pts',(-20.8387067170616,18.9484055163899,
5.49508951239572));
#195484=CARTESIAN_POINT('Ctrl Pts',(-20.7970384789104,18.7266530902619,
5.48023960354974));
#195485=CARTESIAN_POINT('Ctrl Pts',(-20.7732180821995,18.6345335431358,
5.47405981513811));
#195486=CARTESIAN_POINT('Ctrl Pts',(-20.7402342475941,18.5351250499886,
5.46758874833196));
#195487=CARTESIAN_POINT('Ctrl Pts',(-20.7371210654857,18.5259534253344,
5.46699366149591));
#195488=CARTESIAN_POINT('Ctrl Pts',(-20.7324307950927,18.5124409977714,
5.4661201473758));
#195489=CARTESIAN_POINT('Ctrl Pts',(-20.7309023232472,18.508083621821,5.46583896042605));
#195490=CARTESIAN_POINT('Ctrl Pts',(-20.7281650633123,18.5003612139798,
5.46534155039907));
#195491=CARTESIAN_POINT('Ctrl Pts',(-20.7269619964458,18.4969942119751,
5.46512499306352));
#195492=CARTESIAN_POINT('Ctrl Pts',(-20.7243657190294,18.4897857450031,
5.46466204853814));
#195493=CARTESIAN_POINT('Ctrl Pts',(-20.7229699190123,18.4859452717126,
5.46441581796844));
#195494=CARTESIAN_POINT('Ctrl Pts',(-20.7191070449355,18.4754118672103,
5.46374154692406));
#195495=CARTESIAN_POINT('Ctrl Pts',(-20.7166172237732,18.4687272548122,
5.46331484089741));
#195496=CARTESIAN_POINT('Ctrl Pts',(-20.7031297572366,18.4330684877702,
5.46104434321567));
#195497=CARTESIAN_POINT('Ctrl Pts',(-20.6915300445275,18.4043242337992,
5.45923443697878));
#195498=CARTESIAN_POINT('Ctrl Pts',(-20.6147735858126,18.2255379525746,
5.44804385098371));
#195499=CARTESIAN_POINT('Ctrl Pts',(-20.5330352088347,18.083201526635,5.43939871382255));
#195500=CARTESIAN_POINT('Ctrl Pts',(-20.3657123610359,17.8570979885976,
5.42400420355024));
#195501=CARTESIAN_POINT('Ctrl Pts',(-20.2879589510966,17.768522228232,5.41743778955221));
#195502=CARTESIAN_POINT('Ctrl Pts',(-20.1929613279495,17.6769448023356,
5.40970778591301));
#195503=CARTESIAN_POINT('Ctrl Pts',(-20.1825655608044,17.6671245817611,
5.40886565903804));
#195504=CARTESIAN_POINT('Ctrl Pts',(-20.1658644154931,17.6516652604515,
5.4075182737988));
#195505=CARTESIAN_POINT('Ctrl Pts',(-20.1596232412761,17.6459572194073,
5.4070159622059));
#195506=CARTESIAN_POINT('Ctrl Pts',(-20.1485570613703,17.6359574553908,
5.40612733892172));
#195507=CARTESIAN_POINT('Ctrl Pts',(-20.1437462831797,17.6316500980351,
5.40574169427212));
#195508=CARTESIAN_POINT('Ctrl Pts',(-20.1337566233701,17.622787809215,5.40494222486369));
#195509=CARTESIAN_POINT('Ctrl Pts',(-20.1285750443515,17.6182360465067,
5.40452827427119));
#195510=CARTESIAN_POINT('Ctrl Pts',(-20.1152202475009,17.6066196405179,
5.40346318284416));
#195511=CARTESIAN_POINT('Ctrl Pts',(-20.1070151011747,17.5995921574072,
5.40281051482796));
#195512=CARTESIAN_POINT('Ctrl Pts',(-20.0725673216113,17.5705426974243,
5.40007724362974));
#195513=CARTESIAN_POINT('Ctrl Pts',(-20.0458470645127,17.5490975660502,
5.39797336856799));
#195514=CARTESIAN_POINT('Ctrl Pts',(-19.9749015956946,17.4949354874195,
5.39242558435923));
#195515=CARTESIAN_POINT('Ctrl Pts',(-19.9299029427629,17.4632787646679,
5.3889434050106));
#195516=CARTESIAN_POINT('Ctrl Pts',(-19.8068132821667,17.3836656364043,
5.37952163931933));
#195517=CARTESIAN_POINT('Ctrl Pts',(-19.7267585117777,17.3389670105283,
5.37349488361626));
#195518=CARTESIAN_POINT('Ctrl Pts',(-19.5956081871651,17.2765230836912,
5.36389710543965));
#195519=CARTESIAN_POINT('Ctrl Pts',(-19.5462886858002,17.2553014380025,
5.36034708705668));
#195520=CARTESIAN_POINT('Ctrl Pts',(-19.4618385882378,17.2227098381535,
5.3544117276961));
#195521=CARTESIAN_POINT('Ctrl Pts',(-19.4271198685023,17.2103421495578,
5.35201124857902));
#195522=CARTESIAN_POINT('Ctrl Pts',(-19.3471122887055,17.1841743548467,
5.34659330557642));
#195523=CARTESIAN_POINT('Ctrl Pts',(-19.3016451612632,17.170973383084,5.343595801701));
#195524=CARTESIAN_POINT('Ctrl Pts',(-19.248303942376,17.1574080726403,5.34020235095851));
#195525=CARTESIAN_POINT('Ctrl Pts',(-19.2408273098978,17.1555500659615,
5.33972949057989));
#195526=CARTESIAN_POINT('Ctrl Pts',(-19.2288396384694,17.1526404142884,
5.33897596941318));
#195527=CARTESIAN_POINT('Ctrl Pts',(-19.2243350821869,17.1515627079204,
5.33869386801668));
#195528=CARTESIAN_POINT('Ctrl Pts',(-19.2163365248621,17.1496767993993,
5.33819485141022));
#195529=CARTESIAN_POINT('Ctrl Pts',(-19.2128439651575,17.1488626819948,
5.33797759935612));
#195530=CARTESIAN_POINT('Ctrl Pts',(-19.2054209649265,17.1471522525127,
5.33751723502928));
#195531=CARTESIAN_POINT('Ctrl Pts',(-19.2014900368851,17.1462582929048,
5.33727425836989));
#195532=CARTESIAN_POINT('Ctrl Pts',(-19.190838774945,17.1438679928824,5.33661803178459));
#195533=CARTESIAN_POINT('Ctrl Pts',(-19.1841135886215,17.1423931834554,
5.33620599962607));
#195534=CARTESIAN_POINT('Ctrl Pts',(-19.1502449490791,17.135138901002,5.33414202198858));
#195535=CARTESIAN_POINT('Ctrl Pts',(-19.1229955244772,17.1298604541951,
5.33251707659368));
#195536=CARTESIAN_POINT('Ctrl Pts',(-19.0432573198107,17.1160354936811,
5.32784501066362));
#195537=CARTESIAN_POINT('Ctrl Pts',(-18.990538550673,17.1089283747279,5.32485986019752));
#195538=CARTESIAN_POINT('Ctrl Pts',(-18.7974760941367,17.090273908465,5.31412852010918));
#195539=CARTESIAN_POINT('Ctrl Pts',(-18.6563453079949,17.0907452154768,
5.3066446959301));
#195540=CARTESIAN_POINT('Ctrl Pts',(-18.424923898893,17.1146698138369,5.29377537164573));
#195541=CARTESIAN_POINT('Ctrl Pts',(-18.3342673858073,17.1300533091335,
5.28858416500654));
#195542=CARTESIAN_POINT('Ctrl Pts',(-18.2315117169558,17.1544533890304,
5.28239269105735));
#195543=CARTESIAN_POINT('Ctrl Pts',(-18.2181520159386,17.1577637053465,
5.28158175805247));
#195544=CARTESIAN_POINT('Ctrl Pts',(-18.196788139878,17.1632789920246,5.28027501444872));
#195545=CARTESIAN_POINT('Ctrl Pts',(-18.1887628684888,17.1654012180818,
5.27978187592572));
#195546=CARTESIAN_POINT('Ctrl Pts',(-18.174541277107,17.1692516520653,5.27890387653416));
#195547=CARTESIAN_POINT('Ctrl Pts',(-18.1683399297347,17.1709610144871,
5.27851963149954));
#195548=CARTESIAN_POINT('Ctrl Pts',(-18.1554408730214,17.1745798956038,
5.27771744273082));
#195549=CARTESIAN_POINT('Ctrl Pts',(-18.1487446122199,17.1764942530753,
5.27729934529966));
#195550=CARTESIAN_POINT('Ctrl Pts',(-18.1313908689076,17.1815481840478,
5.27621145311304));
#195551=CARTESIAN_POINT('Ctrl Pts',(-18.120748540683,17.184738645085,5.27554000308284));
#195552=CARTESIAN_POINT('Ctrl Pts',(-18.0747485010194,17.1989245737963,
5.27261878435714));
#195553=CARTESIAN_POINT('Ctrl Pts',(-18.0396592970887,17.2107623200322,
5.27034155439784));
#195554=CARTESIAN_POINT('Ctrl Pts',(-17.9473759675078,17.2446160131358,
5.26421777951816));
#195555=CARTESIAN_POINT('Ctrl Pts',(-17.8907997043677,17.2682042025782,
5.26032231174481));
#195556=CARTESIAN_POINT('Ctrl Pts',(-17.6945052438671,17.3602351751819,
5.24632088884511));
#195557=CARTESIAN_POINT('Ctrl Pts',(-17.5613994025567,17.4415702276248,
5.23588323616264));
#195558=CARTESIAN_POINT('Ctrl Pts',(-17.4260086620967,17.5463398278746,
5.22475317908484));
#195559=CARTESIAN_POINT('Ctrl Pts',(-17.4137155305347,17.5560728816246,
5.22373793903934));
#195560=CARTESIAN_POINT('Ctrl Pts',(-17.363772096677,17.5965261950981,5.21959749635092));
#195561=CARTESIAN_POINT('Ctrl Pts',(-17.3270736037052,17.628404316633,5.21651747161211));
#195562=CARTESIAN_POINT('Ctrl Pts',(-17.2858216476618,17.6668080783347,
5.21304209592719));
#195563=CARTESIAN_POINT('Ctrl Pts',(-17.2801703134101,17.6721275303872,
5.21256569186294));
#195564=CARTESIAN_POINT('Ctrl Pts',(-17.2711810731022,17.6806825838358,
5.21180762150207));
#195565=CARTESIAN_POINT('Ctrl Pts',(-17.2678244109493,17.6838982515472,
5.21152448754234));
#195566=CARTESIAN_POINT('Ctrl Pts',(-17.2618953275107,17.6896158573227,
5.21102430209545));
#195567=CARTESIAN_POINT('Ctrl Pts',(-17.259318643427,17.6921133111173,5.21080690817546));
#195568=CARTESIAN_POINT('Ctrl Pts',(-17.2538675405774,17.6974237459058,
5.21034696861655));
#195569=CARTESIAN_POINT('Ctrl Pts',(-17.2509947898639,17.7002383636974,
5.21010455487945));
#195570=CARTESIAN_POINT('Ctrl Pts',(-17.2432564634526,17.7078634387398,
5.20945144187044));
#195571=CARTESIAN_POINT('Ctrl Pts',(-17.2384061106458,17.7126893731268,
5.20904194069538));
#195572=CARTESIAN_POINT('Ctrl Pts',(-17.2143686654116,17.7368388347746,
5.20701133541773));
#195573=CARTESIAN_POINT('Ctrl Pts',(-17.1955313062976,17.7565087586766,
5.20541619656832));
#195574=CARTESIAN_POINT('Ctrl Pts',(-17.1420511874591,17.8145544720225,
5.20085683390368));
#195575=CARTESIAN_POINT('Ctrl Pts',(-17.1084263736188,17.8538440616697,
5.19795107322898));
#195576=CARTESIAN_POINT('Ctrl Pts',(-16.9903960249174,18.0024476766135,
5.18743882826584));
#195577=CARTESIAN_POINT('Ctrl Pts',(-16.915302568965,18.1187108407294,5.18009490839895));
#195578=CARTESIAN_POINT('Ctrl Pts',(-16.8388693379274,18.2670726818203,
5.17088334409471));
#195579=CARTESIAN_POINT('Ctrl Pts',(-16.8261995589176,18.2929496688726,
5.16928315807119));
#195580=CARTESIAN_POINT('Ctrl Pts',(-16.7847811144197,18.3821062485957,
5.16377640171326));
#195581=CARTESIAN_POINT('Ctrl Pts',(-16.7586242460807,18.4465339742871,
5.15980631393645));
#195582=CARTESIAN_POINT('Ctrl Pts',(-16.7314405158915,18.5242614976182,
5.15497298446821));
#195583=CARTESIAN_POINT('Ctrl Pts',(-16.7273073673253,18.5364342692398,
5.1542148743871));
#195584=CARTESIAN_POINT('Ctrl Pts',(-16.7207454755999,18.556354200685,5.15297205301375));
#195585=CARTESIAN_POINT('Ctrl Pts',(-16.71824994359,18.5640791316891,5.15248954647548));
#195586=CARTESIAN_POINT('Ctrl Pts',(-16.713869394972,18.577910606753,5.15162457602174));
#195587=CARTESIAN_POINT('Ctrl Pts',(-16.7119674729204,18.5840117231868,
5.15124267320694));
#195588=CARTESIAN_POINT('Ctrl Pts',(-16.7080022488629,18.5969373460737,
5.15043278364849));
#195589=CARTESIAN_POINT('Ctrl Pts',(-16.7059457420443,18.6037638388475,
5.1500045796847));
#195590=CARTESIAN_POINT('Ctrl Pts',(-16.7005615631578,18.6219688739903,
5.14886131912339));
#195591=CARTESIAN_POINT('Ctrl Pts',(-16.6972949569897,18.6333650783994,
5.14814428039488));
#195592=CARTESIAN_POINT('Ctrl Pts',(-16.6821695114451,18.6878570807787,
5.14470875554201));
#195593=CARTESIAN_POINT('Ctrl Pts',(-16.6715825164489,18.7312912174133,
5.14194941235913));
#195594=CARTESIAN_POINT('Ctrl Pts',(-16.6272657512225,18.9418712911597,
5.12846151811008));
#195595=CARTESIAN_POINT('Ctrl Pts',(-16.6124427002331,19.1123276711236,
5.11714332292881));
#195596=CARTESIAN_POINT('Ctrl Pts',(-16.621593303117,19.3824338143902,5.09933685585448));
#195597=CARTESIAN_POINT('Ctrl Pts',(-16.6320240135644,19.4818381270174,
5.09283065032773));
#195598=CARTESIAN_POINT('Ctrl Pts',(-16.6511231033879,19.5896909190883,
5.08606333908144));
#195599=CARTESIAN_POINT('Ctrl Pts',(-16.6528790946176,19.599225146048,5.08546769257861));
#195600=CARTESIAN_POINT('Ctrl Pts',(-16.6555684523757,19.6132842780257,
5.08459351685813));
#195601=CARTESIAN_POINT('Ctrl Pts',(-16.6564512068669,19.6178185733118,
5.08431222206554));
#195602=CARTESIAN_POINT('Ctrl Pts',(-16.6580435817937,19.6258574875128,
5.08381469282955));
#195603=CARTESIAN_POINT('Ctrl Pts',(-16.658747245999,19.6293632308514,5.08359812353072));
#195604=CARTESIAN_POINT('Ctrl Pts',(-16.6602738691419,19.6368704290137,
5.08313523258017));
#195605=CARTESIAN_POINT('Ctrl Pts',(-16.661099526576,19.6408712784538,5.08288906713493));
#195606=CARTESIAN_POINT('Ctrl Pts',(-16.6633976410968,19.6518465506029,
5.08221515815609));
#195607=CARTESIAN_POINT('Ctrl Pts',(-16.6648937659527,19.6588160396763,
5.08178874668404));
#195608=CARTESIAN_POINT('Ctrl Pts',(-16.6730678008468,19.6959779764364,
5.07952262902255));
#195609=CARTESIAN_POINT('Ctrl Pts',(-16.6803717895789,19.7260306471612,
5.07771665357997));
#195610=CARTESIAN_POINT('Ctrl Pts',(-16.7044696619843,19.8164967108193,
5.07233159790743));
#195611=CARTESIAN_POINT('Ctrl Pts',(-16.7232918049739,19.8763370294956,
5.06883925126178));
#195612=CARTESIAN_POINT('Ctrl Pts',(-16.790731393191,20.0615675883191,5.05800552873976));
#195613=CARTESIAN_POINT('Ctrl Pts',(-16.8486437203579,20.1832090829031,
5.05083714358614));
#195614=CARTESIAN_POINT('Ctrl Pts',(-16.9386589113094,20.3335435202024,
5.04111267647721));
#195615=CARTESIAN_POINT('Ctrl Pts',(-16.9606248620693,20.3679329946825,
5.03882559446556));
#195616=CARTESIAN_POINT('Ctrl Pts',(-17.0109103046547,20.4418590277526,
5.0337442185717));
#195617=CARTESIAN_POINT('Ctrl Pts',(-17.039625252565,20.4810967389569,5.03093809825814));
#195618=CARTESIAN_POINT('Ctrl Pts',(-17.0774530845912,20.5292185647056,
5.02733816105284));
#195619=CARTESIAN_POINT('Ctrl Pts',(-17.0853307458046,20.5390578101946,
5.02659344170211));
#195620=CARTESIAN_POINT('Ctrl Pts',(-17.0979524461682,20.5545370122096,
5.02540774250612));
#195621=CARTESIAN_POINT('Ctrl Pts',(-17.1026389595176,20.5602236490171,
5.0249690860262));
#195622=CARTESIAN_POINT('Ctrl Pts',(-17.1114263488112,20.5707735892956,
5.024149493574));
#195623=CARTESIAN_POINT('Ctrl Pts',(-17.1155196515059,20.5756431137293,
5.02376886934872));
#195624=CARTESIAN_POINT('Ctrl Pts',(-17.1246595324915,20.5864172426741,
5.02292148873999));
#195625=CARTESIAN_POINT('Ctrl Pts',(-17.1297167666524,20.5923126497999,
5.02245429618397));
#195626=CARTESIAN_POINT('Ctrl Pts',(-17.1445047884387,20.6093608418579,
5.02109291545512));
#195627=CARTESIAN_POINT('Ctrl Pts',(-17.1543200885094,20.6204394032361,
5.02019521998889));
#195628=CARTESIAN_POINT('Ctrl Pts',(-17.2331999161843,20.7076122787318,
5.01302595550519));
#195629=CARTESIAN_POINT('Ctrl Pts',(-17.3075955090041,20.7786779026841,
5.00652387157226));
#195630=CARTESIAN_POINT('Ctrl Pts',(-17.5065788343861,20.9428249866548,
4.98977988397894));
#195631=CARTESIAN_POINT('Ctrl Pts',(-17.6368012799828,21.0281218309275,
4.97934997649047));
#195632=CARTESIAN_POINT('Ctrl Pts',(-17.8225521353499,21.1224852809525,
4.96588653368759));
#195633=CARTESIAN_POINT('Ctrl Pts',(-17.8708260118443,21.1447644328443,
4.96250866569724));
#195634=CARTESIAN_POINT('Ctrl Pts',(-17.927930024996,21.1685535829485,4.95869269202706));
#195635=CARTESIAN_POINT('Ctrl Pts',(-17.9359894236675,21.1718528656594,
4.95815821153822));
#195636=CARTESIAN_POINT('Ctrl Pts',(-17.9482261428433,21.1767742804217,
4.95735312975509));
#195637=CARTESIAN_POINT('Ctrl Pts',(-17.9523885185259,21.1784329897204,
4.95708039841341));
#195638=CARTESIAN_POINT('Ctrl Pts',(-17.9598709084113,21.1813872334743,
4.95659218076007));
#195639=CARTESIAN_POINT('Ctrl Pts',(-17.9631889406447,21.1826876049821,
4.95637640718105));
#195640=CARTESIAN_POINT('Ctrl Pts',(-17.9704075447413,21.185495644199,4.95590855402465));
#195641=CARTESIAN_POINT('Ctrl Pts',(-17.9743092922424,21.1870001305491,
4.95565666615287));
#195642=CARTESIAN_POINT('Ctrl Pts',(-17.9852859597766,21.1911953387302,
4.95495075583882));
#195643=CARTESIAN_POINT('Ctrl Pts',(-17.992370971887,21.1938597232629,4.95449828370537));
#195644=CARTESIAN_POINT('Ctrl Pts',(-18.0349027137804,21.2095943235298,
4.95180013023445));
#195645=CARTESIAN_POINT('Ctrl Pts',(-18.0706822325096,21.2217526508862,
4.94960525857077));
#195646=CARTESIAN_POINT('Ctrl Pts',(-18.1897098418822,21.2586762774794,
4.94248968232339));
#195647=CARTESIAN_POINT('Ctrl Pts',(-18.2741606569895,21.2792794972006,
4.93773445267811));
#195648=CARTESIAN_POINT('Ctrl Pts',(-18.5325898067884,21.3257100581067,
4.92344744838294));
#195649=CARTESIAN_POINT('Ctrl Pts',(-18.708709659957,21.3351276809138,4.91400184991385));
#195650=CARTESIAN_POINT('Ctrl Pts',(-18.9068829755556,21.3210541231441,
4.90245711757418));
#195651=CARTESIAN_POINT('Ctrl Pts',(-18.9297731782077,21.3190535400526,
4.90111100529415));
#195652=CARTESIAN_POINT('Ctrl Pts',(-18.9621183921039,21.3156952470103,
4.89918922482309));
#195653=CARTESIAN_POINT('Ctrl Pts',(-18.9716042424459,21.31464547941,4.89862323096034));
#195654=CARTESIAN_POINT('Ctrl Pts',(-18.9870082007834,21.3128352572332,
4.89770010637923));
#195655=CARTESIAN_POINT('Ctrl Pts',(-18.9929308300284,21.3121138527817,
4.89734421060249));
#195656=CARTESIAN_POINT('Ctrl Pts',(-19.0053240500873,21.31055110342,4.89659743474413));
#195657=CARTESIAN_POINT('Ctrl Pts',(-19.0117939501177,21.3097048615339,
4.89620640354894));
#195658=CARTESIAN_POINT('Ctrl Pts',(-19.0271804165713,21.3076199660945,
4.89527362367147));
#195659=CARTESIAN_POINT('Ctrl Pts',(-19.0360931435943,21.3063543298372,
4.89473102680214));
#195660=CARTESIAN_POINT('Ctrl Pts',(-19.0661121620077,21.3018960227297,
4.89289567225049));
#195661=CARTESIAN_POINT('Ctrl Pts',(-19.08717762895,21.2984410593016,4.89159464672465));
#195662=CARTESIAN_POINT('Ctrl Pts',(-19.2017081389943,21.2778735867718,
4.88444734441149));
#195663=CARTESIAN_POINT('Ctrl Pts',(-19.2939803393657,21.2548040864345,
4.87841292982892));
#195664=CARTESIAN_POINT('Ctrl Pts',(-19.5249047939371,21.1802545194414,
4.86264634674662));
#195665=CARTESIAN_POINT('Ctrl Pts',(-19.6602866100661,21.1203149804039,
4.85274046139437));
#195666=CARTESIAN_POINT('Ctrl Pts',(-19.8387282544129,21.017832256677,4.83940174197861));
#195667=CARTESIAN_POINT('Ctrl Pts',(-19.8879220787456,20.9868188126646,
4.83569642376248));
#195668=CARTESIAN_POINT('Ctrl Pts',(-19.9431004681535,20.948769864667,4.83156047351002));
#195669=CARTESIAN_POINT('Ctrl Pts',(-19.9503880085439,20.9436766183176,
4.83101466060256));
#195670=CARTESIAN_POINT('Ctrl Pts',(-19.9613316517685,20.9359250548254,
4.83019593874698));
#195671=CARTESIAN_POINT('Ctrl Pts',(-19.9650115766698,20.9333007655976,
4.82992079274058));
#195672=CARTESIAN_POINT('Ctrl Pts',(-19.9714971904929,20.9286442311516,
4.82943618907267));
#195673=CARTESIAN_POINT('Ctrl Pts',(-19.9743063144003,20.9266168710783,
4.82922640143909));
#195674=CARTESIAN_POINT('Ctrl Pts',(-19.9771213840895,20.9245746918649,
4.82901628298026));
#195675=CARTESIAN_POINT('Ctrl Pts',(-19.9771322559639,20.9245668047563,
4.82901547149881));
#195676=CARTESIAN_POINT('Ctrl Pts',(-19.9771538170015,20.9245511627754,
4.82901386217678));
#195677=CARTESIAN_POINT('Ctrl Pts',(-19.9771645062719,20.9245434078307,
4.82901306432817));
#195678=CARTESIAN_POINT('Ctrl Pts',(-19.977185704677,20.924528028325,4.82901148207944));
#195679=CARTESIAN_POINT('Ctrl Pts',(-19.9771962144594,20.9245204032991,
4.82901069763093));
#195680=CARTESIAN_POINT('Ctrl Pts',(-19.9772164300653,20.9245057362493,
4.82900918874423));
#195681=CARTESIAN_POINT('Ctrl Pts',(-19.9772261348795,20.9244986949795,
4.82900846438115));
#195682=CARTESIAN_POINT('Ctrl Pts',(-19.9772455073426,20.9244846391535,
4.8290070184316));
#195683=CARTESIAN_POINT('Ctrl Pts',(-19.9772551754023,20.9244776243004,
4.82900629681446));
#195684=CARTESIAN_POINT('Ctrl Pts',(-19.977274474704,20.9244636210586,4.82900485633081));
#195685=CARTESIAN_POINT('Ctrl Pts',(-19.9772841061407,20.9244566325296,
4.82900413744976));
#195686=CARTESIAN_POINT('Ctrl Pts',(-19.9773033339959,20.9244426806331,
4.82900270230395));
#195687=CARTESIAN_POINT('Ctrl Pts',(-19.9773129298098,20.9244357177053,
4.82900198608432));
#195688=CARTESIAN_POINT('Ctrl Pts',(-19.9773320848734,20.9244218181358,
4.8290005563767));
#195689=CARTESIAN_POINT('Ctrl Pts',(-19.9773416447492,20.9244148810407,
4.82899984284198));
#195690=CARTESIAN_POINT('Ctrl Pts',(-19.9806435439003,20.9220188256811,
4.82875339450335));
#195691=CARTESIAN_POINT('Ctrl Pts',(-19.9839290220744,20.9196201999858,
4.82850832208095));
#195692=CARTESIAN_POINT('Ctrl Pts',(-19.9907205618502,20.9146318346662,
4.82800198893054));
#195693=CARTESIAN_POINT('Ctrl Pts',(-19.9942255837985,20.9120407042059,
4.82774082473892));
#195694=CARTESIAN_POINT('Ctrl Pts',(-20.00311784422,20.9054244216732,4.82707855560906));
#195695=CARTESIAN_POINT('Ctrl Pts',(-20.0084939965409,20.9013843582822,
4.82667844274994));
#195696=CARTESIAN_POINT('Ctrl Pts',(-20.0239444708727,20.8896580437905,
4.82552910110643));
#195697=CARTESIAN_POINT('Ctrl Pts',(-20.0339693309556,20.8819067361304,
4.82478402985981));
#195698=CARTESIAN_POINT('Ctrl Pts',(-20.0681294779319,20.8550002796233,
4.82224515033091));
#195699=CARTESIAN_POINT('Ctrl Pts',(-20.0919168302753,20.8354077246413,
4.82047716128688));
#195700=CARTESIAN_POINT('Ctrl Pts',(-20.2105264225643,20.7332874393822,
4.81161260447306));
#195701=CARTESIAN_POINT('Ctrl Pts',(-20.298297160638,20.6429457611615,4.80487727607783));
#195702=CARTESIAN_POINT('Ctrl Pts',(-20.4010751592956,20.516352032551,4.79600101221062));
#195703=CARTESIAN_POINT('Ctrl Pts',(-20.4238409329932,20.4867433303909,
4.7939614558361));
#195704=CARTESIAN_POINT('Ctrl Pts',(-20.5058258214295,20.3740679454682,
4.78628948996169));
#195705=CARTESIAN_POINT('Ctrl Pts',(-20.5597935310681,20.2873679217427,
4.78055349557371));
#195706=CARTESIAN_POINT('Ctrl Pts',(-20.6138280496349,20.1847206731101,
4.7737553243962));
#195707=CARTESIAN_POINT('Ctrl Pts',(-20.6202333679171,20.1722539274884,
4.77292973281338));
#195708=CARTESIAN_POINT('Ctrl Pts',(-20.630267537414,20.1522377847369,4.77160387778149));
#195709=CARTESIAN_POINT('Ctrl Pts',(-20.6339762618876,20.1447287304431,
4.77110641393081));
#195710=CARTESIAN_POINT('Ctrl Pts',(-20.6404595832993,20.1314033804103,
4.77022342143287));
#195711=CARTESIAN_POINT('Ctrl Pts',(-20.6432523783057,20.1255960200773,
4.76983853270947));
#195712=CARTESIAN_POINT('Ctrl Pts',(-20.6489941600182,20.1135156033417,
4.76903770671365));
#195713=CARTESIAN_POINT('Ctrl Pts',(-20.6519389351825,20.1072406408504,
4.76862162915387));
#195714=CARTESIAN_POINT('Ctrl Pts',(-20.6594606048486,20.091006023374,4.76754483042365));
#195715=CARTESIAN_POINT('Ctrl Pts',(-20.6639910183447,20.081025174366,4.76688251676034));
#195716=CARTESIAN_POINT('Ctrl Pts',(-20.6829282360487,20.0384291676282,
4.76405428130858));
#195717=CARTESIAN_POINT('Ctrl Pts',(-20.696586664511,20.0054895457633,4.76186301747051));
#195718=CARTESIAN_POINT('Ctrl Pts',(-20.7139016543125,19.9605563628427,
4.75886649057087));
#195719=CARTESIAN_POINT('Ctrl Pts',(-20.7182932737024,19.9488519165805,
4.75808528715504));
#195720=CARTESIAN_POINT('Ctrl Pts',(-20.7225806084094,19.937110297309,4.75730094873459));
#195721=CARTESIAN_POINT('Ctrl Pts',(-20.7225805792317,19.9371103772171,
4.53222349041431));
#195722=CARTESIAN_POINT('Ctrl Pts',(-20.713233383926,19.9627093104351,4.53397185385458));
#195723=CARTESIAN_POINT('Ctrl Pts',(-20.7033905938547,19.988131302222,4.53573318148791));
#195724=CARTESIAN_POINT('Ctrl Pts',(-20.6611588232326,20.0912449146023,
4.54297538962527));
#195725=CARTESIAN_POINT('Ctrl Pts',(-20.6246459300555,20.1671532397865,
4.54854123331881));
#195726=CARTESIAN_POINT('Ctrl Pts',(-20.5387210126306,20.3215080464049,
4.56021214034759));
#195727=CARTESIAN_POINT('Ctrl Pts',(-20.4884753735683,20.3993032970082,
4.56630397075444));
#195728=CARTESIAN_POINT('Ctrl Pts',(-20.414586493627,20.498750912961,4.57416792408563));
#195729=CARTESIAN_POINT('Ctrl Pts',(-20.3953160225471,20.5235176923286,
4.57613279091625));
#195730=CARTESIAN_POINT('Ctrl Pts',(-20.3709791670432,20.5534006409387,
4.57850227352807));
#195731=CARTESIAN_POINT('Ctrl Pts',(-20.3664291607147,20.5589300103313,
4.5789406521064));
#195732=CARTESIAN_POINT('Ctrl Pts',(-20.3592348472954,20.5675830007218,
4.57962644155925));
#195733=CARTESIAN_POINT('Ctrl Pts',(-20.3566094380522,20.5707221623957,
4.5798751854453));
#195734=CARTESIAN_POINT('Ctrl Pts',(-20.3516737613268,20.5765890227675,
4.58033994428915));
#195735=CARTESIAN_POINT('Ctrl Pts',(-20.3493657145128,20.579318451889,4.58055610820751));
#195736=CARTESIAN_POINT('Ctrl Pts',(-20.3440663781821,20.5855531972313,
4.58104977617908));
#195737=CARTESIAN_POINT('Ctrl Pts',(-20.3410705547958,20.5890545950724,
4.58132694207588));
#195738=CARTESIAN_POINT('Ctrl Pts',(-20.3331962608604,20.5981971526258,
4.58205054214663));
#195739=CARTESIAN_POINT('Ctrl Pts',(-20.3282993228531,20.6038224200755,
4.58249564882668));
#195740=CARTESIAN_POINT('Ctrl Pts',(-20.2953704986368,20.6412475904341,
4.58545713018297));
#195741=CARTESIAN_POINT('Ctrl Pts',(-20.2664165505378,20.6722275878557,
4.58790944825523));
#195742=CARTESIAN_POINT('Ctrl Pts',(-20.1846186047802,20.7546415068214,
4.59450432799614));
#195743=CARTESIAN_POINT('Ctrl Pts',(-20.1299864055226,20.8042190182788,
4.59855349281472));
#195744=CARTESIAN_POINT('Ctrl Pts',(-20.0037168815403,20.907313456531,4.60743693862741));
#195745=CARTESIAN_POINT('Ctrl Pts',(-19.9310563503755,20.9593467060511,
4.61224964925924));
#195746=CARTESIAN_POINT('Ctrl Pts',(-19.794950098171,21.0443414970298,4.62107285801276));
#195747=CARTESIAN_POINT('Ctrl Pts',(-19.7327130127349,21.0789741100068,
4.62504159397318));
#195748=CARTESIAN_POINT('Ctrl Pts',(-19.6444797582201,21.122400948149,4.63066725320784));
#195749=CARTESIAN_POINT('Ctrl Pts',(-19.6198784643942,21.1339264747538,
4.63223545290629));
#195750=CARTESIAN_POINT('Ctrl Pts',(-19.5768896153128,21.1530663830061,
4.63497946636038));
#195751=CARTESIAN_POINT('Ctrl Pts',(-19.5586036068405,21.1609009183432,
4.6361478028167));
#195752=CARTESIAN_POINT('Ctrl Pts',(-19.5321442687545,21.1717985170344,
4.63784107725754));
#195753=CARTESIAN_POINT('Ctrl Pts',(-19.5240578219808,21.1750707045843,
4.63835893208218));
#195754=CARTESIAN_POINT('Ctrl Pts',(-19.5099047252628,21.180696219467,4.63926601681111));
#195755=CARTESIAN_POINT('Ctrl Pts',(-19.5038469813823,21.1830717439957,
4.63965449265329));
#195756=CARTESIAN_POINT('Ctrl Pts',(-19.492193445895,21.1875797627123,4.64040229919977));
#195757=CARTESIAN_POINT('Ctrl Pts',(-19.4865993615355,21.1897165182595,
4.64076148220421));
#195758=CARTESIAN_POINT('Ctrl Pts',(-19.4719543225548,21.1952393512042,
4.64170239407505));
#195759=CARTESIAN_POINT('Ctrl Pts',(-19.4628891923829,21.1985872120307,
4.64228539472868));
#195760=CARTESIAN_POINT('Ctrl Pts',(-19.4315146219173,21.2099307115649,
4.64430536920633));
#195761=CARTESIAN_POINT('Ctrl Pts',(-19.4090946836316,21.2176134988925,
4.64575266831049));
#195762=CARTESIAN_POINT('Ctrl Pts',(-19.230923269086,21.2753447296468,4.6572887560153));
#195763=CARTESIAN_POINT('Ctrl Pts',(-19.0700025548621,21.307553127075,4.66797862973147));
#195764=CARTESIAN_POINT('Ctrl Pts',(-18.7784687148216,21.3314590686806,
4.68730861918814));
#195765=CARTESIAN_POINT('Ctrl Pts',(-18.6492150723303,21.3302315799233,
4.69584464570825));
#195766=CARTESIAN_POINT('Ctrl Pts',(-18.5089911857911,21.3160421626598,
4.7045850312468));
#195767=CARTESIAN_POINT('Ctrl Pts',(-18.4971256831738,21.314740013913,4.70532038278404));
#195768=CARTESIAN_POINT('Ctrl Pts',(-18.4802789760351,21.3127468725763,
4.70635779451977));
#195769=CARTESIAN_POINT('Ctrl Pts',(-18.4752884926774,21.3121384132326,
4.70666427576211));
#195770=CARTESIAN_POINT('Ctrl Pts',(-18.4666941808978,21.3110594770468,
4.70719059281528));
#195771=CARTESIAN_POINT('Ctrl Pts',(-18.4630893251251,21.3105974888244,
4.70741090303321));
#195772=CARTESIAN_POINT('Ctrl Pts',(-18.4561039183034,21.3096839684002,
4.70783691937066));
#195773=CARTESIAN_POINT('Ctrl Pts',(-18.4527232689363,21.309233550486,4.70804268954486));
#195774=CARTESIAN_POINT('Ctrl Pts',(-18.4436089685325,21.3079967910042,
4.70859639529961));
#195775=CARTESIAN_POINT('Ctrl Pts',(-18.4378773803075,21.307195097918,4.7089434702055));
#195776=CARTESIAN_POINT('Ctrl Pts',(-18.4166388038024,21.3041355503146,
4.71022562629459));
#195777=CARTESIAN_POINT('Ctrl Pts',(-18.4011533056921,21.3017289808452,
4.71115267728231));
#195778=CARTESIAN_POINT('Ctrl Pts',(-18.2523765728645,21.276912948643,4.71999644537115));
#195779=CARTESIAN_POINT('Ctrl Pts',(-18.1214744451817,21.2419554305564,
4.72730362917144));
#195780=CARTESIAN_POINT('Ctrl Pts',(-17.8486617835098,21.140295868747,4.74311376677318));
#195781=CARTESIAN_POINT('Ctrl Pts',(-17.7090202495407,21.069874744594,4.75160379699766));
#195782=CARTESIAN_POINT('Ctrl Pts',(-17.5605587937187,20.9731513297329,
4.76192279316519));
#195783=CARTESIAN_POINT('Ctrl Pts',(-17.5429107640739,20.9612708238939,
4.76317118101039));
#195784=CARTESIAN_POINT('Ctrl Pts',(-17.51806424711,20.9439945362681,4.76496137328442));
#195785=CARTESIAN_POINT('Ctrl Pts',(-17.5107161160549,20.9388154859171,
4.76549493859828));
#195786=CARTESIAN_POINT('Ctrl Pts',(-17.4980937156258,20.9297981857111,
4.76641874720204));
#195787=CARTESIAN_POINT('Ctrl Pts',(-17.4928037498933,20.9259820448658,
4.76680813617712));
#195788=CARTESIAN_POINT('Ctrl Pts',(-17.4827068992902,20.9186270684645,
4.76755567312621));
#195789=CARTESIAN_POINT('Ctrl Pts',(-17.4778971727331,20.9150922260942,
4.76791366367569));
#195790=CARTESIAN_POINT('Ctrl Pts',(-17.4654248415636,20.9058443649018,
4.76884696658883));
#195791=CARTESIAN_POINT('Ctrl Pts',(-17.4577859267834,20.9000997568169,
4.76942351087295));
#195792=CARTESIAN_POINT('Ctrl Pts',(-17.4318482850916,20.8803177645991,
4.77139821373091));
#195793=CARTESIAN_POINT('Ctrl Pts',(-17.4137406663534,20.8660335687672,
4.77280608768999));
#195794=CARTESIAN_POINT('Ctrl Pts',(-17.2606270958368,20.7411380080771,
4.78496908566283));
#195795=CARTESIAN_POINT('Ctrl Pts',(-17.1395693085175,20.6145375798855,
4.79641924003365));
#195796=CARTESIAN_POINT('Ctrl Pts',(-16.9831019959069,20.4042031917327,
4.81374051816536));
#195797=CARTESIAN_POINT('Ctrl Pts',(-16.9351842757812,20.3306613782542,
4.81952114923206));
#195798=CARTESIAN_POINT('Ctrl Pts',(-16.873238946879,20.2212973608538,4.82754699855225));
#195799=CARTESIAN_POINT('Ctrl Pts',(-16.8554062532793,20.1877386570312,
4.82993711797288));
#195800=CARTESIAN_POINT('Ctrl Pts',(-16.8351092762402,20.1469276131491,
4.83274195447701));
#195801=CARTESIAN_POINT('Ctrl Pts',(-16.831769646756,20.1401211788707,4.83320640702422));
#195802=CARTESIAN_POINT('Ctrl Pts',(-16.8266436340144,20.1295304578039,
4.83392375458381));
#195803=CARTESIAN_POINT('Ctrl Pts',(-16.8248318236553,20.1257586479018,
4.83417818853336));
#195804=CARTESIAN_POINT('Ctrl Pts',(-16.821497732587,20.118764714034,4.83464801097033));
#195805=CARTESIAN_POINT('Ctrl Pts',(-16.8199724173638,20.115544146028,4.83486358236687));
#195806=CARTESIAN_POINT('Ctrl Pts',(-16.8165490113443,20.1082684947465,
4.83534885497302));
#195807=CARTESIAN_POINT('Ctrl Pts',(-16.8146556536927,20.1042112441671,
4.83561826209147));
#195808=CARTESIAN_POINT('Ctrl Pts',(-16.8091242923405,20.0922593653788,
4.8364084348112));
#195809=CARTESIAN_POINT('Ctrl Pts',(-16.8055219729698,20.0843481918064,
4.83692705227377));
#195810=CARTESIAN_POINT('Ctrl Pts',(-16.7804002270661,20.0282641025753,
4.84057408257743));
#195811=CARTESIAN_POINT('Ctrl Pts',(-16.7606376636852,19.9793194423272,
4.84360334408258));
#195812=CARTESIAN_POINT('Ctrl Pts',(-16.737302674407,19.9146645052183,4.84747088431362));
#195813=CARTESIAN_POINT('Ctrl Pts',(-16.7320521465366,19.8995846034768,
4.8483636327534));
#195814=CARTESIAN_POINT('Ctrl Pts',(-16.7108619521275,19.8364328889333,
4.85206901272793));
#195815=CARTESIAN_POINT('Ctrl Pts',(-16.6964788235245,19.7878549712471,
4.85483964212562));
#195816=CARTESIAN_POINT('Ctrl Pts',(-16.6565744201966,19.6328550733939,
4.86355394811894));
#195817=CARTESIAN_POINT('Ctrl Pts',(-16.6375521563209,19.5249495248811,
4.86944480571278));
#195818=CARTESIAN_POINT('Ctrl Pts',(-16.6216101786746,19.3611428764858,
4.87859557618059));
#195819=CARTESIAN_POINT('Ctrl Pts',(-16.618414858479,19.3060394768938,4.88170678099319));
#195820=CARTESIAN_POINT('Ctrl Pts',(-16.6167287868548,19.2165444817433,
4.88685635292515));
#195821=CARTESIAN_POINT('Ctrl Pts',(-16.6169174162056,19.1822029936109,
4.88885522061801));
#195822=CARTESIAN_POINT('Ctrl Pts',(-16.6182634844682,19.1370749970996,
4.89151787542284));
#195823=CARTESIAN_POINT('Ctrl Pts',(-16.6186686424979,19.1262701315257,
4.89215808886423));
#195824=CARTESIAN_POINT('Ctrl Pts',(-16.6194678676687,19.1085770685749,
4.89321104958199));
#195825=CARTESIAN_POINT('Ctrl Pts',(-16.6198128721122,19.1016867707712,
4.89362225411417));
#195826=CARTESIAN_POINT('Ctrl Pts',(-16.620545944099,19.088351558327,4.89442034858492));
#195827=CARTESIAN_POINT('Ctrl Pts',(-16.6209298286186,19.0819064833734,
4.89480710281834));
#195828=CARTESIAN_POINT('Ctrl Pts',(-16.6218843617584,19.0670278472426,
4.89570234673728));
#195829=CARTESIAN_POINT('Ctrl Pts',(-16.6224760472178,19.0585957885613,
4.89621149193062));
#195830=CARTESIAN_POINT('Ctrl Pts',(-16.6242033429986,19.0359254990372,
4.89758528708301));
#195831=CARTESIAN_POINT('Ctrl Pts',(-16.6254325647706,19.0216950339365,
4.898452861707));
#195832=CARTESIAN_POINT('Ctrl Pts',(-16.6403645156076,18.86709465359,4.9079366001282));
#195833=CARTESIAN_POINT('Ctrl Pts',(-16.6679152092711,18.7284435548166,
4.91700231892608));
#195834=CARTESIAN_POINT('Ctrl Pts',(-16.7372072757883,18.5011836776805,
4.9326328377619));
#195835=CARTESIAN_POINT('Ctrl Pts',(-16.7716712806174,18.4108209019477,
4.93905852807083));
#195836=CARTESIAN_POINT('Ctrl Pts',(-16.8327336459496,18.2786504652834,
4.94855953930433));
#195837=CARTESIAN_POINT('Ctrl Pts',(-16.8548209919588,18.2348973958161,
4.95172133382279));
#195838=CARTESIAN_POINT('Ctrl Pts',(-16.8910494056186,18.1689291004062,
4.95647396021502));
#195839=CARTESIAN_POINT('Ctrl Pts',(-16.9041185930277,18.146146565785,4.95811246632818));
#195840=CARTESIAN_POINT('Ctrl Pts',(-16.9210812293672,18.1178118972069,
4.9601410656946));
#195841=CARTESIAN_POINT('Ctrl Pts',(-16.9245812673146,18.1120284127145,
4.96055463808154));
#195842=CARTESIAN_POINT('Ctrl Pts',(-16.9301981844756,18.1028465637965,
4.96121031500938));
#195843=CARTESIAN_POINT('Ctrl Pts',(-16.9322970701134,18.0994373247938,
4.96145356817236));
#195844=CARTESIAN_POINT('Ctrl Pts',(-16.936297953282,18.0929797583861,4.96191390996638));
#195845=CARTESIAN_POINT('Ctrl Pts',(-16.9381980157753,18.0899303576313,
4.96213111362045));
#195846=CARTESIAN_POINT('Ctrl Pts',(-16.9425917585578,18.0829186954831,
4.96263015238819));
#195847=CARTESIAN_POINT('Ctrl Pts',(-16.945090824282,18.0789598597652,4.96291162780119));
#195848=CARTESIAN_POINT('Ctrl Pts',(-16.9518285652205,18.0683644560912,
4.96366429101311));
#195849=CARTESIAN_POINT('Ctrl Pts',(-16.9560912175355,18.0617431206457,
4.96413393484555));
#195850=CARTESIAN_POINT('Ctrl Pts',(-16.9884162903409,18.0121416767099,
4.96764793965742));
#195851=CARTESIAN_POINT('Ctrl Pts',(-17.0179990733392,17.9701674146237,
4.97059806226464));
#195852=CARTESIAN_POINT('Ctrl Pts',(-17.0626452480492,17.9114753802039,
4.97475229737124));
#195853=CARTESIAN_POINT('Ctrl Pts',(-17.0764918968775,17.8938599612684,
4.97600306807218));
#195854=CARTESIAN_POINT('Ctrl Pts',(-17.1195448496476,17.8408432492152,
4.97979050055642));
#195855=CARTESIAN_POINT('Ctrl Pts',(-17.1496253632879,17.8061682644905,
4.98229989190679));
#195856=CARTESIAN_POINT('Ctrl Pts',(-17.255114675471,17.6922685963979,4.99075210937858));
#195857=CARTESIAN_POINT('Ctrl Pts',(-17.3355233671548,17.6179183626198,
4.99664031276523));
#195858=CARTESIAN_POINT('Ctrl Pts',(-17.4645505988168,17.5159411090446,
5.00578491209592));
#195859=CARTESIAN_POINT('Ctrl Pts',(-17.5091045416287,17.483470869543,5.00889257928465));
#195860=CARTESIAN_POINT('Ctrl Pts',(-17.5833667270592,17.4336679624074,
5.0140368177582));
#195861=CARTESIAN_POINT('Ctrl Pts',(-17.6123201843384,17.4152549470559,
5.01603399682121));
#195862=CARTESIAN_POINT('Ctrl Pts',(-17.6509662748633,17.3919772442362,
5.01869472080579));
#195863=CARTESIAN_POINT('Ctrl Pts',(-17.6602678796239,17.3864712490936,
5.0193347356674));
#195864=CARTESIAN_POINT('Ctrl Pts',(-17.6755740158714,17.377568511949,5.02038745294817));
#195865=CARTESIAN_POINT('Ctrl Pts',(-17.6815537795617,17.3741294175667,
5.02079861402289));
#195866=CARTESIAN_POINT('Ctrl Pts',(-17.6931630205272,17.3675279842937,
5.02159668358584));
#195867=CARTESIAN_POINT('Ctrl Pts',(-17.6987903733775,17.3643620500906,
5.02198345668368));
#195868=CARTESIAN_POINT('Ctrl Pts',(-17.7118195196232,17.3571101579072,
5.0228788308503));
#195869=CARTESIAN_POINT('Ctrl Pts',(-17.7192314456833,17.3530427187341,
5.02338808802767));
#195870=CARTESIAN_POINT('Ctrl Pts',(-17.7392357772361,17.3422203616659,
5.02476238128829));
#195871=CARTESIAN_POINT('Ctrl Pts',(-17.7518723723176,17.3355484536332,
5.02563034533766));
#195872=CARTESIAN_POINT('Ctrl Pts',(-17.8684363630794,17.2755057766444,
5.03363648433267));
#195873=CARTESIAN_POINT('Ctrl Pts',(-17.976530576028,17.2307044244463,5.04107633799039));
#195874=CARTESIAN_POINT('Ctrl Pts',(-18.2426514564894,17.1453947565814,
5.05933040839353));
#195875=CARTESIAN_POINT('Ctrl Pts',(-18.4027530446898,17.1137580179814,
5.07028453074278));
#195876=CARTESIAN_POINT('Ctrl Pts',(-18.5973725200904,17.0981622479942,
5.0826915602721));
#195877=CARTESIAN_POINT('Ctrl Pts',(-18.6299059532684,17.0963096836068,
5.0847336114845));
#195878=CARTESIAN_POINT('Ctrl Pts',(-18.6697115475675,17.0949639705341,
5.08718279188374));
#195879=CARTESIAN_POINT('Ctrl Pts',(-18.6769532641206,17.0947563570008,
5.08762636912633));
#195880=CARTESIAN_POINT('Ctrl Pts',(-18.6883056354449,17.0944892102064,
5.08831845917592));
#195881=CARTESIAN_POINT('Ctrl Pts',(-18.6924155611055,17.0944044710028,
5.0885683450577));
#195882=CARTESIAN_POINT('Ctrl Pts',(-18.7000969193988,17.0942684774893,
5.08903408517602));
#195883=CARTESIAN_POINT('Ctrl Pts',(-18.7036681956824,17.0942142906892,
5.08925009527308));
#195884=CARTESIAN_POINT('Ctrl Pts',(-18.7118190225153,17.094111250438,5.08974191909529));
#195885=CARTESIAN_POINT('Ctrl Pts',(-18.7163985961855,17.094068219032,5.09001740418829));
#195886=CARTESIAN_POINT('Ctrl Pts',(-18.7304693501879,17.0939816681184,
5.09086132563016));
#195887=CARTESIAN_POINT('Ctrl Pts',(-18.7399608629648,17.0939871141838,
5.09142709314652));
#195888=CARTESIAN_POINT('Ctrl Pts',(-18.8249031590651,17.0946071339047,
5.09646148737402));
#195889=CARTESIAN_POINT('Ctrl Pts',(-18.9002795819994,17.0991913405416,
5.10072611330635));
#195890=CARTESIAN_POINT('Ctrl Pts',(-19.0180423249742,17.1126998415495,
5.1072883759256));
#195891=CARTESIAN_POINT('Ctrl Pts',(-19.0606682227336,17.1189121287575,
5.10964260969806));
#195892=CARTESIAN_POINT('Ctrl Pts',(-19.2107261167275,17.1454799597475,
5.11793932390216));
#195893=CARTESIAN_POINT('Ctrl Pts',(-19.3167371133434,17.1728495155747,
5.12382617277009));
#195894=CARTESIAN_POINT('Ctrl Pts',(-19.4722621403519,17.2261343217636,
5.13296762309385));
#195895=CARTESIAN_POINT('Ctrl Pts',(-19.5236485237689,17.2460121341427,
5.13607348535374));
#195896=CARTESIAN_POINT('Ctrl Pts',(-19.6056761766708,17.2814804463411,
5.14121500240233));
#195897=CARTESIAN_POINT('Ctrl Pts',(-19.6368166268502,17.2958532675417,
5.1432113196033));
#195898=CARTESIAN_POINT('Ctrl Pts',(-19.6772926816756,17.3157415176362,
5.1458710580706));
#195899=CARTESIAN_POINT('Ctrl Pts',(-19.6869555650449,17.3205816646126,
5.14651097151932));
#195900=CARTESIAN_POINT('Ctrl Pts',(-19.7027243744774,17.328631899363,5.14756356448092));
#195901=CARTESIAN_POINT('Ctrl Pts',(-19.7088524956181,17.3317982572225,
5.14797470336404));
#195902=CARTESIAN_POINT('Ctrl Pts',(-19.7206869043408,17.3379864802095,
5.14877276022434));
#195903=CARTESIAN_POINT('Ctrl Pts',(-19.7263950627273,17.3410046175037,
5.14915954297188));
#195904=CARTESIAN_POINT('Ctrl Pts',(-19.7395461324536,17.3480353002705,
5.15005498372877));
#195905=CARTESIAN_POINT('Ctrl Pts',(-19.7469789523099,17.3520663982091,
5.15056429815377));
#195906=CARTESIAN_POINT('Ctrl Pts',(-19.7669104229469,17.3630310213209,
5.1519388460782));
#195907=CARTESIAN_POINT('Ctrl Pts',(-19.7793631677644,17.370046681812,5.15280700923223));
#195908=CARTESIAN_POINT('Ctrl Pts',(-19.8931596885263,17.4356845638511,
5.16082846320481));
#195909=CARTESIAN_POINT('Ctrl Pts',(-19.9895317027028,17.5024835750581,
5.16828477314389));
#195910=CARTESIAN_POINT('Ctrl Pts',(-20.2060423060182,17.6808053590924,
5.18660785684195));
#195911=CARTESIAN_POINT('Ctrl Pts',(-20.3197459716108,17.7989751811815,
5.19761657700647));
#195912=CARTESIAN_POINT('Ctrl Pts',(-20.4378942683944,17.9542439776002,
5.21000427536224));
#195913=CARTESIAN_POINT('Ctrl Pts',(-20.4564998273439,17.9798680120139,
5.21198742626012));
#195914=CARTESIAN_POINT('Ctrl Pts',(-20.4786123357413,18.0118051192277,
5.21437581782508));
#195915=CARTESIAN_POINT('Ctrl Pts',(-20.4826700050878,18.0177297955606,
5.21481544872758));
#195916=CARTESIAN_POINT('Ctrl Pts',(-20.488995177713,18.0270668475793,5.21550275631196));
#195917=CARTESIAN_POINT('Ctrl Pts',(-20.4912830116499,18.0304652902939,
5.21575177561123));
#195918=CARTESIAN_POINT('Ctrl Pts',(-20.4955481618066,18.0368407919681,
5.21621676934283));
#195919=CARTESIAN_POINT('Ctrl Pts',(-20.4975277822605,18.039816182837,5.21643289440411));
#195920=CARTESIAN_POINT('Ctrl Pts',(-20.5020388918464,18.0466338002259,
5.21692610958048));
#195921=CARTESIAN_POINT('Ctrl Pts',(-20.5045653910778,18.0504792689952,
5.21720286387093));
#195922=CARTESIAN_POINT('Ctrl Pts',(-20.511141568415,18.0605600304962,5.21792468320672));
#195923=CARTESIAN_POINT('Ctrl Pts',(-20.5151710118547,18.0668085353283,
5.21836843136674));
#195924=CARTESIAN_POINT('Ctrl Pts',(-20.5417163990186,18.1084528422731,
5.22130250108755));
#195925=CARTESIAN_POINT('Ctrl Pts',(-20.5632105518177,18.1444925692471,
5.22373010620223));
#195926=CARTESIAN_POINT('Ctrl Pts',(-20.5941836418223,18.200120543654,5.22734779879829));
#195927=CARTESIAN_POINT('Ctrl Pts',(-20.6044541275495,18.2192531246507,
5.22856960795265));
#195928=CARTESIAN_POINT('Ctrl Pts',(-20.6222719321328,18.2537071279278,
5.23073593038642));
#195929=CARTESIAN_POINT('Ctrl Pts',(-20.6299315080533,18.2689680108981,
5.23168382475274));
#195930=CARTESIAN_POINT('Ctrl Pts',(-20.6957490246493,18.4041575655516,
5.23999255929711));
#195931=CARTESIAN_POINT('Ctrl Pts',(-20.742645368146,18.5292378966341,5.24709271865252));
#195932=CARTESIAN_POINT('Ctrl Pts',(-20.8031161572572,18.7526519636485,
5.25986490638718));
#195933=CARTESIAN_POINT('Ctrl Pts',(-20.8221382508542,18.8490612180803,
5.26540011154393));
#195934=CARTESIAN_POINT('Ctrl Pts',(-20.8362368145887,18.9609907704941,
5.27201872403664));
#195935=CARTESIAN_POINT('Ctrl Pts',(-20.8379188833009,18.9755651773305,
5.27288406086351));
#195936=CARTESIAN_POINT('Ctrl Pts',(-20.8402567481172,18.9978535229694,
5.2742132233605));
#195937=CARTESIAN_POINT('Ctrl Pts',(-20.8410219631316,19.0055557153255,
5.27467360114129));
#195938=CARTESIAN_POINT('Ctrl Pts',(-20.8422815026533,19.0189814911236,
5.27547799829814));
#195939=CARTESIAN_POINT('Ctrl Pts',(-20.8427948027886,19.0247032450434,
5.27582141648292));
#195940=CARTESIAN_POINT('Ctrl Pts',(-20.8438966146373,19.037573578127,5.27659527622887));
#195941=CARTESIAN_POINT('Ctrl Pts',(-20.8444720950536,19.0447231757292,
5.27702612346942));
#195942=CARTESIAN_POINT('Ctrl Pts',(-20.8459169690494,19.0638914689281,
5.27818387553732));
#195943=CARTESIAN_POINT('Ctrl Pts',(-20.8467200885576,19.0759147599919,
5.27891285187492));
#195944=CARTESIAN_POINT('Ctrl Pts',(-20.8498276623778,19.1292856925848,
5.28216148649077));
#195945=CARTESIAN_POINT('Ctrl Pts',(-20.8510211083768,19.1706865674428,
5.28471565814259));
#195946=CARTESIAN_POINT('Ctrl Pts',(-20.8509121657631,19.3815723388986,
5.29790828090238));
#195947=CARTESIAN_POINT('Ctrl Pts',(-20.8304727772938,19.5504051994466,
5.30913945498687));
#195948=CARTESIAN_POINT('Ctrl Pts',(-20.771698414488,19.7902026692572,5.32541888131401));
#195949=CARTESIAN_POINT('Ctrl Pts',(-20.7491431302945,19.8643641701078,
5.33048906851518));
#195950=CARTESIAN_POINT('Ctrl Pts',(-20.7225805912209,19.9371103443827,
5.33540100209138));
#195951=CARTESIAN_POINT('Origin',(-18.734,19.211,0.));
#195952=CARTESIAN_POINT('',(-20.7225806064499,19.9371103026755,6.3535037140067));
#195953=CARTESIAN_POINT('',(-20.7225806064498,19.9371103026755,6.13370788222325));
#195954=CARTESIAN_POINT('',(-20.7225806064498,19.9371103026755,0.));
#195955=CARTESIAN_POINT('',(-20.8509995791047,19.2123349421389,6.31236858093732));
#195956=CARTESIAN_POINT('Ctrl Pts',(-20.7225806064498,19.9371103026756,
6.35350371400671));
#195957=CARTESIAN_POINT('Ctrl Pts',(-20.7235885970627,19.9343497433268,
6.35332822035437));
#195958=CARTESIAN_POINT('Ctrl Pts',(-20.724590846667,19.9315870649596,6.35315305116633));
#195959=CARTESIAN_POINT('Ctrl Pts',(-20.7384657750112,19.8930912808199,
6.35071847537167));
#195960=CARTESIAN_POINT('Ctrl Pts',(-20.7503812099478,19.857017630369,6.34851222594941));
#195961=CARTESIAN_POINT('Ctrl Pts',(-20.7865572725681,19.736716450352,6.34134105663081));
#195962=CARTESIAN_POINT('Ctrl Pts',(-20.8065607469455,19.6512993602537,
6.33654457769394));
#195963=CARTESIAN_POINT('Ctrl Pts',(-20.8409626152498,19.4483957315726,
6.32534846007863));
#195964=CARTESIAN_POINT('Ctrl Pts',(-20.8509250852906,19.3304699297772,
6.31898334375529));
#195965=CARTESIAN_POINT('Ctrl Pts',(-20.8509995791047,19.2123349421389,
6.31236858093732));
#195966=CARTESIAN_POINT('Ctrl Pts',(-20.85099958079,19.2123322668744,6.3123684311405));
#195967=CARTESIAN_POINT('Ctrl Pts',(-20.8510434843996,19.1425685244161,
6.30846212993567));
#195968=CARTESIAN_POINT('Ctrl Pts',(-20.8476389261171,19.0728498012217,
6.30447848065918));
#195969=CARTESIAN_POINT('Ctrl Pts',(-20.8397869279037,18.9931536601121,
6.29977940203969));
#195970=CARTESIAN_POINT('Ctrl Pts',(-20.8386993799332,18.9828857128295,
6.29917123854736));
#195971=CARTESIAN_POINT('Ctrl Pts',(-20.8367363709343,18.9655630760309,
6.29814042520597));
#195972=CARTESIAN_POINT('Ctrl Pts',(-20.8359004048649,18.9585040288362,
6.29771901463873));
#195973=CARTESIAN_POINT('Ctrl Pts',(-20.8342948980459,18.9455076569588,
6.29694061396329));
#195974=CARTESIAN_POINT('Ctrl Pts',(-20.8335356902283,18.9395691113789,
6.29658395236896));
#195975=CARTESIAN_POINT('Ctrl Pts',(-20.8319163682403,18.9273161565484,
6.29584599643015));
#195976=CARTESIAN_POINT('Ctrl Pts',(-20.8310529127544,18.9210022570801,
6.29546459999048));
#195977=CARTESIAN_POINT('Ctrl Pts',(-20.8290506673527,18.9068378254571,
6.2946064050122));
#195978=CARTESIAN_POINT('Ctrl Pts',(-20.8278962379869,18.8989896330738,
6.29412911596063));
#195979=CARTESIAN_POINT('Ctrl Pts',(-20.8248469162425,18.8790388038057,
6.29291118497491));
#195980=CARTESIAN_POINT('Ctrl Pts',(-20.8228910539935,18.8669459089206,
6.29216862077348));
#195981=CARTESIAN_POINT('Ctrl Pts',(-20.8108421494137,18.7963422494321,
6.28780728121338));
#195982=CARTESIAN_POINT('Ctrl Pts',(-20.7983969467989,18.7382648606237,
6.28411428556892));
#195983=CARTESIAN_POINT('Ctrl Pts',(-20.768184864996,18.6214796440378,6.27646782283292));
#195984=CARTESIAN_POINT('Ctrl Pts',(-20.7502747202371,18.5628660550676,
6.27251334280754));
#195985=CARTESIAN_POINT('Ctrl Pts',(-20.6755356481374,18.3515455583173,
6.25787182674141));
#195986=CARTESIAN_POINT('Ctrl Pts',(-20.6036810235824,18.2047616685174,
6.24690184082058));
#195987=CARTESIAN_POINT('Ctrl Pts',(-20.4982581648339,18.0404761583438,
6.23450060265955));
#195988=CARTESIAN_POINT('Ctrl Pts',(-20.4801870803267,18.0136847196447,
6.23247583529186));
#195989=CARTESIAN_POINT('Ctrl Pts',(-20.4573317969455,17.981419285517,6.23004447346033));
#195990=CARTESIAN_POINT('Ctrl Pts',(-20.4531247089344,17.9755440297639,
6.22960204057148));
#195991=CARTESIAN_POINT('Ctrl Pts',(-20.446479581814,17.9663636889624,6.22891133710014));
#195992=CARTESIAN_POINT('Ctrl Pts',(-20.4440619140411,17.9630440249385,
6.22866170230413));
#195993=CARTESIAN_POINT('Ctrl Pts',(-20.4395231336304,17.9568498486629,
6.22819617957426));
#195994=CARTESIAN_POINT('Ctrl Pts',(-20.4374044286747,17.9539737019274,
6.22798013729281));
#195995=CARTESIAN_POINT('Ctrl Pts',(-20.432549214559,17.9474175548383,6.22748791547497));
#195996=CARTESIAN_POINT('Ctrl Pts',(-20.4298080270493,17.9437410815849,
6.22721206663253));
#195997=CARTESIAN_POINT('Ctrl Pts',(-20.4213381391625,17.9324579860471,
6.22636592169027));
#195998=CARTESIAN_POINT('Ctrl Pts',(-20.4155699543542,17.9248809644555,
6.22579831488482));
#195999=CARTESIAN_POINT('Ctrl Pts',(-20.3366220007337,17.8226149958194,
6.21814184625226));
#196000=CARTESIAN_POINT('Ctrl Pts',(-20.2555812996749,17.7342437984343,
6.21157123568353));
#196001=CARTESIAN_POINT('Ctrl Pts',(-20.0873438689919,17.5794322826007,
6.19912687077946));
#196002=CARTESIAN_POINT('Ctrl Pts',(-20.0016214805514,17.5119744870199,
6.19325974339119));
#196003=CARTESIAN_POINT('Ctrl Pts',(-19.8657158327931,17.4210589894665,
6.18416411522203));
#196004=CARTESIAN_POINT('Ctrl Pts',(-19.8191841601983,17.3924719535463,
6.18108449626243));
#196005=CARTESIAN_POINT('Ctrl Pts',(-19.7518700138761,17.3546212427312,
6.17664065565643));
#196006=CARTESIAN_POINT('Ctrl Pts',(-19.7319619168714,17.3438434954631,
6.17532783861267));
#196007=CARTESIAN_POINT('Ctrl Pts',(-19.6966134116401,17.3254335294786,
6.17299694498611));
#196008=CARTESIAN_POINT('Ctrl Pts',(-19.6812453606778,17.3176665122917,
6.17198361600958));
#196009=CARTESIAN_POINT('Ctrl Pts',(-19.6584068545006,17.3064715867414,
6.1704770517554));
#196010=CARTESIAN_POINT('Ctrl Pts',(-19.6510081966836,17.3028982013879,
6.16998889345795));
#196011=CARTESIAN_POINT('Ctrl Pts',(-19.6380627616575,17.2967385297406,
6.16913451216844));
#196012=CARTESIAN_POINT('Ctrl Pts',(-19.6325251896346,17.2941330416762,
6.16876896054389));
#196013=CARTESIAN_POINT('Ctrl Pts',(-19.6214722476851,17.2889909305909,
6.16803913168097));
#196014=CARTESIAN_POINT('Ctrl Pts',(-19.6159571092058,17.2864539471269,
6.16767487125934));
#196015=CARTESIAN_POINT('Ctrl Pts',(-19.6027565128356,17.2804502841944,
6.16680274611347));
#196016=CARTESIAN_POINT('Ctrl Pts',(-19.5950611519647,17.2770057463499,
6.16629412584133));
#196017=CARTESIAN_POINT('Ctrl Pts',(-19.5672754632262,17.2647672400747,
6.16445676650978));
#196018=CARTESIAN_POINT('Ctrl Pts',(-19.5470698885699,17.2562398477201,
6.1631189813563));
#196019=CARTESIAN_POINT('Ctrl Pts',(-19.3530644998931,17.1778917720344,
6.15025414341361));
#196020=CARTESIAN_POINT('Ctrl Pts',(-19.1708837222702,17.131126405521,6.13791080300001));
#196021=CARTESIAN_POINT('Ctrl Pts',(-18.9064965828143,17.0995593735971,
6.12033449500081));
#196022=CARTESIAN_POINT('Ctrl Pts',(-18.8275435838399,17.094590807783,6.11514392804049));
#196023=CARTESIAN_POINT('Ctrl Pts',(-18.7127636716571,17.0938049993789,
6.10782890704954));
#196024=CARTESIAN_POINT('Ctrl Pts',(-18.6770312462052,17.0944649628788,
6.10558452811651));
#196025=CARTESIAN_POINT('Ctrl Pts',(-18.6338894366461,17.0963552666428,
6.10292790187064));
#196026=CARTESIAN_POINT('Ctrl Pts',(-18.626450186497,17.096720568464,6.10247171559809));
#196027=CARTESIAN_POINT('Ctrl Pts',(-18.6148637028832,17.0973508310434,
6.10176436104888));
#196028=CARTESIAN_POINT('Ctrl Pts',(-18.610715144731,17.0975887499428,6.10151172047072));
#196029=CARTESIAN_POINT('Ctrl Pts',(-18.603007484209,17.0980535551069,6.10104353885059));
#196030=CARTESIAN_POINT('Ctrl Pts',(-18.5994482888448,17.0982772175513,
6.10082782548917));
#196031=CARTESIAN_POINT('Ctrl Pts',(-18.5913834213461,17.0988044825677,
6.10034011094005));
#196032=CARTESIAN_POINT('Ctrl Pts',(-18.5868781566768,17.0991135076777,
6.10006841686534));
#196033=CARTESIAN_POINT('Ctrl Pts',(-18.575238981094,17.0999492881576,6.09936838369463));
#196034=CARTESIAN_POINT('Ctrl Pts',(-18.5681066227213,17.1004977944205,
6.09894123492731));
#196035=CARTESIAN_POINT('Ctrl Pts',(-18.5241278525014,17.1041042556274,
6.09631790102283));
#196036=CARTESIAN_POINT('Ctrl Pts',(-18.4873615789615,17.1080910962504,
6.09417027794141));
#196037=CARTESIAN_POINT('Ctrl Pts',(-18.2817962903531,17.1358482011441,
6.08232481103278));
#196038=CARTESIAN_POINT('Ctrl Pts',(-18.1162345485755,17.1789761287412,
6.07335635840107));
#196039=CARTESIAN_POINT('Ctrl Pts',(-17.8691055451318,17.276394120929,6.05874253821852));
#196040=CARTESIAN_POINT('Ctrl Pts',(-17.7830487507644,17.3172125272942,
6.05340688478541));
#196041=CARTESIAN_POINT('Ctrl Pts',(-17.6813933922093,17.3741100527393,
6.04662317454197));
#196042=CARTESIAN_POINT('Ctrl Pts',(-17.6629118486344,17.3848249065455,
6.04536966723941));
#196043=CARTESIAN_POINT('Ctrl Pts',(-17.6368750407788,17.4004512126132,
6.0435734000358));
#196044=CARTESIAN_POINT('Ctrl Pts',(-17.6291837195674,17.4051342601596,
6.04303895689151));
#196045=CARTESIAN_POINT('Ctrl Pts',(-17.6159707144262,17.413295324851,6.04211410897012));
#196046=CARTESIAN_POINT('Ctrl Pts',(-17.6104347629344,17.4167500901378,
6.04172456370628));
#196047=CARTESIAN_POINT('Ctrl Pts',(-17.5998684001713,17.4234122103324,
6.04097706212021));
#196048=CARTESIAN_POINT('Ctrl Pts',(-17.5948353933899,17.4266153471257,
6.04061926483872));
#196049=CARTESIAN_POINT('Ctrl Pts',(-17.5817888909255,17.4349961755454,
6.03968720272675));
#196050=CARTESIAN_POINT('Ctrl Pts',(-17.573796803638,17.4402067983973,6.03911171244558));
#196051=CARTESIAN_POINT('Ctrl Pts',(-17.5466940638271,17.4581392887053,
6.03714446346937));
#196052=CARTESIAN_POINT('Ctrl Pts',(-17.5277557729903,17.471117573238,6.03574308840025));
#196053=CARTESIAN_POINT('Ctrl Pts',(-17.3655108966283,17.5862251519348,
6.0234989959911));
#196054=CARTESIAN_POINT('Ctrl Pts',(-17.2352706780062,17.7055291347743,
6.01194819141612));
#196055=CARTESIAN_POINT('Ctrl Pts',(-17.0651619122613,17.9055572688175,
5.99459965398099));
#196056=CARTESIAN_POINT('Ctrl Pts',(-17.0131158677944,17.974973706075,5.98888819890156));
#196057=CARTESIAN_POINT('Ctrl Pts',(-16.9447274514095,18.0789148274861,
5.98094501205016));
#196058=CARTESIAN_POINT('Ctrl Pts',(-16.924830335303,18.1109915351281,5.9785713809598));
#196059=CARTESIAN_POINT('Ctrl Pts',(-16.9019848554932,18.1501198148435,
5.97578326406884));
#196060=CARTESIAN_POINT('Ctrl Pts',(-16.8982045707327,18.1566749064866,
5.97531971527384));
#196061=CARTESIAN_POINT('Ctrl Pts',(-16.8923900894788,18.1668834261588,
5.974603459683));
#196062=CARTESIAN_POINT('Ctrl Pts',(-16.8903314771768,18.1705227724988,
5.97434922129647));
#196063=CARTESIAN_POINT('Ctrl Pts',(-16.8865382088722,18.1772753601127,
5.97387957961708));
#196064=CARTESIAN_POINT('Ctrl Pts',(-16.8848006469526,18.1803868554234,
5.9736639945653));
#196065=CARTESIAN_POINT('Ctrl Pts',(-16.8808958751458,18.187420894747,5.97317846397312));
#196066=CARTESIAN_POINT('Ctrl Pts',(-16.8787332642552,18.1913459300575,
5.97290881390909));
#196067=CARTESIAN_POINT('Ctrl Pts',(-16.8724034036225,18.2029211329634,
5.97211726735905));
#196068=CARTESIAN_POINT('Ctrl Pts',(-16.8682708338209,18.2105902968383,
5.97159753021339));
#196069=CARTESIAN_POINT('Ctrl Pts',(-16.8392385361524,18.2652736667509,
5.96792340350182));
#196070=CARTESIAN_POINT('Ctrl Pts',(-16.8160692644747,18.3131904387904,
5.96486984281173));
#196071=CARTESIAN_POINT('Ctrl Pts',(-16.7880791762991,18.3771199194924,
5.96094459639308));
#196072=CARTESIAN_POINT('Ctrl Pts',(-16.7816085926323,18.3923843066682,
5.96001820504389));
#196073=CARTESIAN_POINT('Ctrl Pts',(-16.7187292951286,18.5457070303135,
5.95080645080096));
#196074=CARTESIAN_POINT('Ctrl Pts',(-16.6768784295116,18.6892863407392,
5.94290170800813));
#196075=CARTESIAN_POINT('Ctrl Pts',(-16.6395521323042,18.8967175714134,
5.93124048580072));
#196076=CARTESIAN_POINT('Ctrl Pts',(-16.6312934351056,18.9578013333906,
5.92778256618447));
#196077=CARTESIAN_POINT('Ctrl Pts',(-16.6223416737196,19.0561772179567,
5.92211326607198));
#196078=CARTESIAN_POINT('Ctrl Pts',(-16.6199487523165,19.0932797601167,
5.91995269090957));
#196079=CARTESIAN_POINT('Ctrl Pts',(-16.6181104870815,19.1415424115342,
5.91710563011443));
#196080=CARTESIAN_POINT('Ctrl Pts',(-16.6177746779774,19.1526633326378,
5.91644708928978));
#196081=CARTESIAN_POINT('Ctrl Pts',(-16.6173711488613,19.1707525170337,
5.91537164258326));
#196082=CARTESIAN_POINT('Ctrl Pts',(-16.6172501428516,19.1777194676155,
5.91495641066516));
#196083=CARTESIAN_POINT('Ctrl Pts',(-16.6170835953851,19.1911178413868,
5.91415583484454));
#196084=CARTESIAN_POINT('Ctrl Pts',(-16.617032962678,19.197549132552,5.91377065508149));
#196085=CARTESIAN_POINT('Ctrl Pts',(-16.6169841377683,19.2122740797372,
5.91288665504818));
#196086=CARTESIAN_POINT('Ctrl Pts',(-16.617005375271,19.2205676554675,5.91238723118004));
#196087=CARTESIAN_POINT('Ctrl Pts',(-16.6171912512708,19.2425983293028,
5.91105643836946));
#196088=CARTESIAN_POINT('Ctrl Pts',(-16.6174408737861,19.2563341415234,
5.910222422906));
#196089=CARTESIAN_POINT('Ctrl Pts',(-16.6203593388622,19.3608943568631,
5.90384010850424));
#196090=CARTESIAN_POINT('Ctrl Pts',(-16.6287390252885,19.4514529004444,
5.89811312666068));
#196091=CARTESIAN_POINT('Ctrl Pts',(-16.664836764059,19.6800641311033,5.88316588084904));
#196092=CARTESIAN_POINT('Ctrl Pts',(-16.7005470077048,19.8164103179136,
5.87376836695336));
#196093=CARTESIAN_POINT('Ctrl Pts',(-16.768326615805,19.9988702428161,5.86102877477234));
#196094=CARTESIAN_POINT('Ctrl Pts',(-16.7890868596193,20.048809671569,5.85752804886356));
#196095=CARTESIAN_POINT('Ctrl Pts',(-16.8234929313602,20.1233809940084,
5.85233226288481));
#196096=CARTESIAN_POINT('Ctrl Pts',(-16.8357543484,20.1486246375683,5.85057920977994));
#196097=CARTESIAN_POINT('Ctrl Pts',(-16.8516566273907,20.1797725080392,
5.84843020079177));
#196098=CARTESIAN_POINT('Ctrl Pts',(-16.8548287155888,20.1859112942341,
5.8480073552443));
#196099=CARTESIAN_POINT('Ctrl Pts',(-16.8599015295176,20.1956117095243,
5.84734041314579));
#196100=CARTESIAN_POINT('Ctrl Pts',(-16.8617824514703,20.1991835594688,
5.84709510035074));
#196101=CARTESIAN_POINT('Ctrl Pts',(-16.8653530515628,20.2059173001764,
5.84663316531952));
#196102=CARTESIAN_POINT('Ctrl Pts',(-16.8670405233587,20.2090802396831,
5.84641641516736));
#196103=CARTESIAN_POINT('Ctrl Pts',(-16.870922073583,20.2163113963391,5.84592137814805));
#196104=CARTESIAN_POINT('Ctrl Pts',(-16.8731214438711,20.2203767204462,
5.84564343141904));
#196105=CARTESIAN_POINT('Ctrl Pts',(-16.8790065080989,20.2311700812277,
5.84490636216305));
#196106=CARTESIAN_POINT('Ctrl Pts',(-16.8827155268657,20.2378854138571,
5.84444868489924));
#196107=CARTESIAN_POINT('Ctrl Pts',(-16.9092561666818,20.2853271602103,
5.84122071899547));
#196108=CARTESIAN_POINT('Ctrl Pts',(-16.933394932927,20.3253118980481,5.83852828084531));
#196109=CARTESIAN_POINT('Ctrl Pts',(-16.9612803690312,20.3682269434661,
5.83563328125264));
#196110=CARTESIAN_POINT('Ctrl Pts',(-16.9637343984861,20.3719775145429,
5.8353802278577));
#196111=CARTESIAN_POINT('Ctrl Pts',(-16.9790341052072,20.3951992414694,
5.83381298876503));
#196112=CARTESIAN_POINT('Ctrl Pts',(-16.9921892848664,20.4144652565201,
5.83251072265505));
#196113=CARTESIAN_POINT('Ctrl Pts',(-17.031938258186,20.4706608691324,5.8286944360761));
#196114=CARTESIAN_POINT('Ctrl Pts',(-17.0594077533745,20.5069555234893,
5.82620624392669));
#196115=CARTESIAN_POINT('Ctrl Pts',(-17.1567931128374,20.6273560458897,
5.81777527866447));
#196116=CARTESIAN_POINT('Ctrl Pts',(-17.2320430416328,20.7069179205334,
5.81188726902176));
#196117=CARTESIAN_POINT('Ctrl Pts',(-17.3539495714906,20.8172959610812,
5.80274312010775));
#196118=CARTESIAN_POINT('Ctrl Pts',(-17.3962267306153,20.8526722980612,
5.7996357110908));
#196119=CARTESIAN_POINT('Ctrl Pts',(-17.4669834455431,20.9073298627378,
5.7944918618775));
#196120=CARTESIAN_POINT('Ctrl Pts',(-17.4946377665465,20.927638287524,5.79249480608614));
#196121=CARTESIAN_POINT('Ctrl Pts',(-17.5316370964553,20.9534492183662,
5.78983422306384));
#196122=CARTESIAN_POINT('Ctrl Pts',(-17.5405490858929,20.9595653374878,
5.78919422271112));
#196123=CARTESIAN_POINT('Ctrl Pts',(-17.5552247276767,20.9694724740131,
5.78814152322078));
#196124=CARTESIAN_POINT('Ctrl Pts',(-17.5609608346986,20.9733040882436,
5.78773036532537));
#196125=CARTESIAN_POINT('Ctrl Pts',(-17.5721021360872,20.9806677780441,
5.78693229759204));
#196126=CARTESIAN_POINT('Ctrl Pts',(-17.5775049705407,20.9842032980501,
5.7865455231215));
#196127=CARTESIAN_POINT('Ctrl Pts',(-17.5900196115848,20.9923111334808,
5.7856501394523));
#196128=CARTESIAN_POINT('Ctrl Pts',(-17.5971427684536,20.9968656486933,
5.78514087410114));
#196129=CARTESIAN_POINT('Ctrl Pts',(-17.6163783330885,21.009003064068,5.78376654446671));
#196130=CARTESIAN_POINT('Ctrl Pts',(-17.6285403917863,21.0165060918307,
5.78289855197605));
#196131=CARTESIAN_POINT('Ctrl Pts',(-17.7408542623367,21.084234634933,5.77489024909518));
#196132=CARTESIAN_POINT('Ctrl Pts',(-17.8457399606368,21.1361838213998,
5.7674480708377));
#196133=CARTESIAN_POINT('Ctrl Pts',(-18.1056903762818,21.2391543620767,
5.74918452659896));
#196134=CARTESIAN_POINT('Ctrl Pts',(-18.2634245468998,21.2814448611377,
5.7382229855241));
#196135=CARTESIAN_POINT('Ctrl Pts',(-18.4565498267117,21.3099910951027,
5.72581868247732));
#196136=CARTESIAN_POINT('Ctrl Pts',(-18.4887612653043,21.313997966307,5.72378473181657));
#196137=CARTESIAN_POINT('Ctrl Pts',(-18.5282532400213,21.3179906570333,
5.72134390059341));
#196138=CARTESIAN_POINT('Ctrl Pts',(-18.5354562325502,21.3186816016554,
5.72090085829218));
#196139=CARTESIAN_POINT('Ctrl Pts',(-18.5467547795702,21.3197069758705,
5.72020941639157));
#196140=CARTESIAN_POINT('Ctrl Pts',(-18.5508479270595,21.3200664288968,
5.71995964786274));
#196141=CARTESIAN_POINT('Ctrl Pts',(-18.5585013383062,21.3207160896551,
5.71949400946267));
#196142=CARTESIAN_POINT('Ctrl Pts',(-18.562061250733,21.3210092004386,5.71927798443774));
#196143=CARTESIAN_POINT('Ctrl Pts',(-18.5701900261697,21.321657786677,5.7187859751206));
#196144=CARTESIAN_POINT('Ctrl Pts',(-18.5747593033939,21.3220074375608,
5.71851032042195));
#196145=CARTESIAN_POINT('Ctrl Pts',(-18.5888100988992,21.3230367545008,
5.71766536263211));
#196146=CARTESIAN_POINT('Ctrl Pts',(-18.5982952388894,21.3236674099768,
5.71709873790055));
#196147=CARTESIAN_POINT('Ctrl Pts',(-18.6836875767826,21.3287675718274,
5.71202892657737));
#196148=CARTESIAN_POINT('Ctrl Pts',(-18.759788751183,21.3292087683342,5.70773293424254));
#196149=CARTESIAN_POINT('Ctrl Pts',(-18.8781801227877,21.3235115463132,
5.7011733252909));
#196150=CARTESIAN_POINT('Ctrl Pts',(-18.9205339217518,21.3201937367961,
5.69885159883338));
#196151=CARTESIAN_POINT('Ctrl Pts',(-19.0714390388761,21.3037910866686,
5.69058745326399));
#196152=CARTESIAN_POINT('Ctrl Pts',(-19.1790385582027,21.2835779676184,
5.6847008706784));
#196153=CARTESIAN_POINT('Ctrl Pts',(-19.337769272666,21.2408238079544,5.67556003937225));
#196154=CARTESIAN_POINT('Ctrl Pts',(-19.3903645313063,21.22443164367,5.6724545318912));
#196155=CARTESIAN_POINT('Ctrl Pts',(-19.4745732107129,21.1945362817295,
5.66731354979412));
#196156=CARTESIAN_POINT('Ctrl Pts',(-19.5066030770277,21.1822810937091,
5.66531740203229));
#196157=CARTESIAN_POINT('Ctrl Pts',(-19.5483165278224,21.1651479942459,
5.66265785732385));
#196158=CARTESIAN_POINT('Ctrl Pts',(-19.5582814048659,21.1609656278861,
5.6620179638236));
#196159=CARTESIAN_POINT('Ctrl Pts',(-19.5745533179218,21.1539891144056,
5.66096539532043));
#196160=CARTESIAN_POINT('Ctrl Pts',(-19.5808795703622,21.1512400806446,
5.6605542608067));
#196161=CARTESIAN_POINT('Ctrl Pts',(-19.5931016127375,21.1458579048335,
5.65975620645533));
#196162=CARTESIAN_POINT('Ctrl Pts',(-19.5989990193485,21.1432286065573,
5.65936942181559));
#196163=CARTESIAN_POINT('Ctrl Pts',(-19.6125913970298,21.1370938858507,
5.65847396797539));
#196164=CARTESIAN_POINT('Ctrl Pts',(-19.6202775402769,21.1335692753205,
5.6579646422989));
#196165=CARTESIAN_POINT('Ctrl Pts',(-19.6408989806712,21.1239630276172,
5.65659004430657));
#196166=CARTESIAN_POINT('Ctrl Pts',(-19.653793968036,21.1177963569317,5.65572184200403));
#196167=CARTESIAN_POINT('Ctrl Pts',(-19.7717736563679,21.05990061519,5.64769732733988));
#196168=CARTESIAN_POINT('Ctrl Pts',(-19.8724412122536,20.9996730816309,
5.64023772750553));
#196169=CARTESIAN_POINT('Ctrl Pts',(-20.100565671935,20.8361020534301,5.6219002579477));
#196170=CARTESIAN_POINT('Ctrl Pts',(-20.2220273583324,20.7256726417926,
5.61087999345474));
#196171=CARTESIAN_POINT('Ctrl Pts',(-20.3502422298733,20.5786404347042,
5.59849616853959));
#196172=CARTESIAN_POINT('Ctrl Pts',(-20.3703945966566,20.5544627919728,
5.59652526307071));
#196173=CARTESIAN_POINT('Ctrl Pts',(-20.394466628494,20.5242368201498,5.59414953339098));
#196174=CARTESIAN_POINT('Ctrl Pts',(-20.3989032659307,20.5186075438063,
5.59371073975647));
#196175=CARTESIAN_POINT('Ctrl Pts',(-20.4058289597471,20.5097277190205,
5.59302444712903));
#196176=CARTESIAN_POINT('Ctrl Pts',(-20.4083372744581,20.5064923584559,
5.59277561194386));
#196177=CARTESIAN_POINT('Ctrl Pts',(-20.4130180116902,20.5004185867781,
5.59231077536583));
#196178=CARTESIAN_POINT('Ctrl Pts',(-20.4151926059839,20.497581982351,5.59209462445893));
#196179=CARTESIAN_POINT('Ctrl Pts',(-20.4201529604497,20.4910775003369,
5.59160110718075));
#196180=CARTESIAN_POINT('Ctrl Pts',(-20.4229339368643,20.4874060367804,
5.59132407819034));
#196181=CARTESIAN_POINT('Ctrl Pts',(-20.430181993639,20.4777719412308,5.59060107055908));
#196182=CARTESIAN_POINT('Ctrl Pts',(-20.4346296633213,20.4717946932659,
5.59015641587812));
#196183=CARTESIAN_POINT('Ctrl Pts',(-20.4640846174746,20.4317705577963,
5.58720408883549));
#196184=CARTESIAN_POINT('Ctrl Pts',(-20.4881014047042,20.3970026724826,
5.58476002387392));
#196185=CARTESIAN_POINT('Ctrl Pts',(-20.5515185183681,20.299051676216,5.57813170930489));
#196186=CARTESIAN_POINT('Ctrl Pts',(-20.5886527365288,20.234471898914,5.57404402846568));
#196187=CARTESIAN_POINT('Ctrl Pts',(-20.6602976389824,20.0931151602238,
5.56540883367988));
#196188=CARTESIAN_POINT('Ctrl Pts',(-20.6937775095326,20.0159926504986,
5.56087765513829));
#196189=CARTESIAN_POINT('Ctrl Pts',(-20.722580628988,19.937110240951,5.55626853452768));
#196190=CARTESIAN_POINT('',(-20.8509995343428,19.212404133962,6.0890562790225));
#196191=CARTESIAN_POINT('Ctrl Pts',(-20.7225805912209,19.9371103443827,
5.33540100209138));
#196192=CARTESIAN_POINT('Ctrl Pts',(-20.7135660345865,19.9617982895418,
5.33706797012045));
#196193=CARTESIAN_POINT('Ctrl Pts',(-20.7040899507275,19.9863232427178,
5.33871648488639));
#196194=CARTESIAN_POINT('Ctrl Pts',(-20.6904971184,20.0196419938108,5.34093976153892));
#196195=CARTESIAN_POINT('Ctrl Pts',(-20.6867761549495,20.028586781516,5.34153499025804));
#196196=CARTESIAN_POINT('Ctrl Pts',(-20.6811908871778,20.0417574708377,
5.34240867211156));
#196197=CARTESIAN_POINT('Ctrl Pts',(-20.6793740071793,20.0460031733982,
5.342689886409));
#196198=CARTESIAN_POINT('Ctrl Pts',(-20.6761257889705,20.053525491649,5.34318732666474));
#196199=CARTESIAN_POINT('Ctrl Pts',(-20.6747000297133,20.0568044570775,
5.34340388703281));
#196200=CARTESIAN_POINT('Ctrl Pts',(-20.6716271655759,20.0638227612115,
5.34386681796256));
#196201=CARTESIAN_POINT('Ctrl Pts',(-20.6699775451052,20.067560937888,5.34411303200905));
#196202=CARTESIAN_POINT('Ctrl Pts',(-20.6654189064737,20.0778107467186,
5.34478721117637));
#196203=CARTESIAN_POINT('Ctrl Pts',(-20.6624877592546,20.0843125606631,
5.34521384245481));
#196204=CARTESIAN_POINT('Ctrl Pts',(-20.6466515865044,20.1189715090635,
5.34748322760273));
#196205=CARTESIAN_POINT('Ctrl Pts',(-20.6331619181897,20.1468592785305,
5.34929213537687));
#196206=CARTESIAN_POINT('Ctrl Pts',(-20.5446480095021,20.3200449097339,
5.36047878659695));
#196207=CARTESIAN_POINT('Ctrl Pts',(-20.4536052171951,20.4565509095654,
5.36912130513015));
#196208=CARTESIAN_POINT('Ctrl Pts',(-20.2715338366188,20.6709803975028,
5.38451644388529));
#196209=CARTESIAN_POINT('Ctrl Pts',(-20.1879783781721,20.7542091843604,
5.39108669184648));
#196210=CARTESIAN_POINT('Ctrl Pts',(-20.0870076702794,20.8392701787546,
5.39882101046907));
#196211=CARTESIAN_POINT('Ctrl Pts',(-20.075977228451,20.8483730895036,5.3996631879519));
#196212=CARTESIAN_POINT('Ctrl Pts',(-20.058277885152,20.8626805446235,5.40101063904461));
#196213=CARTESIAN_POINT('Ctrl Pts',(-20.0516684383127,20.8679581835696,
5.40151296542724));
#196214=CARTESIAN_POINT('Ctrl Pts',(-20.039957501663,20.8771949770625,5.40240160594772));
#196215=CARTESIAN_POINT('Ctrl Pts',(-20.0348691625804,20.8811706853371,
5.40278725296098));
#196216=CARTESIAN_POINT('Ctrl Pts',(-20.0243087481201,20.8893443927697,
5.4035867185068));
#196217=CARTESIAN_POINT('Ctrl Pts',(-20.0188341943366,20.8935390508185,
5.40400066282992));
#196218=CARTESIAN_POINT('Ctrl Pts',(-20.0047322464095,20.9042351454735,
5.40506571968163));
#196219=CARTESIAN_POINT('Ctrl Pts',(-19.9960754864076,20.9106973729951,
5.4057183592004));
#196220=CARTESIAN_POINT('Ctrl Pts',(-19.9597641693583,20.9373732387904,
5.40845135447529));
#196221=CARTESIAN_POINT('Ctrl Pts',(-19.9316717813474,20.9569795094198,
5.41055497623381));
#196222=CARTESIAN_POINT('Ctrl Pts',(-19.857271187706,21.0062646145043,5.41610193348169));
#196223=CARTESIAN_POINT('Ctrl Pts',(-19.8102625012957,21.0348342603711,
5.41958352494815));
#196224=CARTESIAN_POINT('Ctrl Pts',(-19.6666534953555,21.1146263806904,
5.4301425048208));
#196225=CARTESIAN_POINT('Ctrl Pts',(-19.5671475887808,21.1602299932548,
5.43736831881349));
#196226=CARTESIAN_POINT('Ctrl Pts',(-19.4286063014337,21.2111699333928,
5.44711919345343));
#196227=CARTESIAN_POINT('Ctrl Pts',(-19.3922842171244,21.2234163749141,
5.44964693207065));
#196228=CARTESIAN_POINT('Ctrl Pts',(-19.3246533106698,21.2441918430126,
5.45428210398152));
#196229=CARTESIAN_POINT('Ctrl Pts',(-19.2934416935216,21.253000376649,5.45639373279736));
#196230=CARTESIAN_POINT('Ctrl Pts',(-19.25593813785,21.262660125563,5.45888980568219));
#196231=CARTESIAN_POINT('Ctrl Pts',(-19.249830177726,21.2642043054003,5.45929502693071));
#196232=CARTESIAN_POINT('Ctrl Pts',(-19.2015192301592,21.2761888179575,
5.46248943829245));
#196233=CARTESIAN_POINT('Ctrl Pts',(-19.1590072001206,21.2853549748665,
5.46523622537189));
#196234=CARTESIAN_POINT('Ctrl Pts',(-19.1088498456021,21.2945625851522,
5.46837909211825));
#196235=CARTESIAN_POINT('Ctrl Pts',(-19.1014525170888,21.2958798777215,
5.46884012772329));
#196236=CARTESIAN_POINT('Ctrl Pts',(-19.0894908303876,21.297944335113,5.46958145635208));
#196237=CARTESIAN_POINT('Ctrl Pts',(-19.0849308383423,21.2987159615205,
5.46986308398426));
#196238=CARTESIAN_POINT('Ctrl Pts',(-19.0768402819635,21.3000577613761,
5.47036098142376));
#196239=CARTESIAN_POINT('Ctrl Pts',(-19.073310767816,21.3006339375186,5.47057758792936));
#196240=CARTESIAN_POINT('Ctrl Pts',(-19.0657496693643,21.3018485878729,
5.4710403148354));
#196241=CARTESIAN_POINT('Ctrl Pts',(-19.0617177047297,21.302484345432,5.47128628030116));
#196242=CARTESIAN_POINT('Ctrl Pts',(-19.0506547154868,21.3041959734194,
5.47195907772502));
#196243=CARTESIAN_POINT('Ctrl Pts',(-19.0436199936327,21.3052480881673,
5.47238458493671));
#196244=CARTESIAN_POINT('Ctrl Pts',(-19.0061840729049,21.3106542596439,
5.47463731965919));
#196245=CARTESIAN_POINT('Ctrl Pts',(-18.9756944251468,21.3143820877623,
5.47643128668597));
#196246=CARTESIAN_POINT('Ctrl Pts',(-18.8834083949871,21.3236320781564,
5.48176744818545));
#196247=CARTESIAN_POINT('Ctrl Pts',(-18.8214372885932,21.3271032599958,
5.48522475002098));
#196248=CARTESIAN_POINT('Ctrl Pts',(-18.6125869234852,21.3296091649353,
5.49670838165205));
#196249=CARTESIAN_POINT('Ctrl Pts',(-18.465992946418,21.3160935516277,5.50451808001055));
#196250=CARTESIAN_POINT('Ctrl Pts',(-18.2486289311332,21.2729639755249,
5.51689097089301));
#196251=CARTESIAN_POINT('Ctrl Pts',(-18.1761119603627,21.2545360753492,
5.52115152578509));
#196252=CARTESIAN_POINT('Ctrl Pts',(-18.0922002379856,21.2284127449467,
5.52630815978251));
#196253=CARTESIAN_POINT('Ctrl Pts',(-18.0797105919105,21.2243967509875,
5.52708163424079));
#196254=CARTESIAN_POINT('Ctrl Pts',(-18.0594783470984,21.2176830216465,
5.52834463408212));
#196255=CARTESIAN_POINT('Ctrl Pts',(-18.0517125571541,21.2150559004289,
5.52883183202753));
#196256=CARTESIAN_POINT('Ctrl Pts',(-18.0379118724071,21.2102976962042,
5.52970203066707));
#196257=CARTESIAN_POINT('Ctrl Pts',(-18.0318709826287,21.2081842180928,
5.53008444386483));
#196258=CARTESIAN_POINT('Ctrl Pts',(-18.0191632818446,21.2036734953266,
5.53089211289025));
#196259=CARTESIAN_POINT('Ctrl Pts',(-18.0124987464797,21.2012701153033,
5.53131756916379));
#196260=CARTESIAN_POINT('Ctrl Pts',(-17.9949047563192,21.194825346598,5.53244577956629));
#196261=CARTESIAN_POINT('Ctrl Pts',(-17.9839965041616,21.1907271359354,
5.5331504247071));
#196262=CARTESIAN_POINT('Ctrl Pts',(-17.9334956544943,21.1712767773999,
5.53643707146966));
#196263=CARTESIAN_POINT('Ctrl Pts',(-17.8943391386625,21.1548265048645,
5.53905575800747));
#196264=CARTESIAN_POINT('Ctrl Pts',(-17.787868518414,21.1062791072656,5.54637750231929));
#196265=CARTESIAN_POINT('Ctrl Pts',(-17.72171900158,21.0717882666089,5.55115661438224));
#196266=CARTESIAN_POINT('Ctrl Pts',(-17.5531236676056,20.9722275716033,
5.56391168800682));
#196267=CARTESIAN_POINT('Ctrl Pts',(-17.4542113403519,20.9017189459469,
5.57200186061405));
#196268=CARTESIAN_POINT('Ctrl Pts',(-17.3030462510381,20.7730593194106,
5.58499180765804));
#196269=CARTESIAN_POINT('Ctrl Pts',(-17.246990504661,20.7197953368602,5.58997006572426));
#196270=CARTESIAN_POINT('Ctrl Pts',(-17.1874400658751,20.6566596653488,
5.59533057441974));
#196271=CARTESIAN_POINT('Ctrl Pts',(-17.1809592735439,20.6496952448621,
5.59591495009343));
#196272=CARTESIAN_POINT('Ctrl Pts',(-17.1714254380028,20.6393104533852,
5.59677578992672));
#196273=CARTESIAN_POINT('Ctrl Pts',(-17.1683363077027,20.6359235827177,
5.59705490177421));
#196274=CARTESIAN_POINT('Ctrl Pts',(-17.1628595701602,20.6298796670671,
5.59755002693678));
#196275=CARTESIAN_POINT('Ctrl Pts',(-17.1604676675143,20.6272265917477,
5.59776636301128));
#196276=CARTESIAN_POINT('Ctrl Pts',(-17.1553394962875,20.6215094430481,
5.59823037956115));
#196277=CARTESIAN_POINT('Ctrl Pts',(-17.1526054354679,20.6184434648815,
5.59847789530395));
#196278=CARTESIAN_POINT('Ctrl Pts',(-17.1450830115729,20.6099582195034,
5.59915932034447));
#196279=CARTESIAN_POINT('Ctrl Pts',(-17.1403134134999,20.6045222866787,
5.599591847653));
#196280=CARTESIAN_POINT('Ctrl Pts',(-17.1143338902617,20.5746054619374,
5.6019510564018));
#196281=CARTESIAN_POINT('Ctrl Pts',(-17.0936588560968,20.5496632710242,
5.60384063874464));
#196282=CARTESIAN_POINT('Ctrl Pts',(-16.9725697307351,20.3965621157053,
5.61505004650333));
#196283=CARTESIAN_POINT('Ctrl Pts',(-16.8866325848176,20.2576325301369,
5.62365501079258));
#196284=CARTESIAN_POINT('Ctrl Pts',(-16.7678204063314,20.0044022091073,
5.63896791783413));
#196285=CARTESIAN_POINT('Ctrl Pts',(-16.7270298344355,19.8946773723757,
5.64549249748144));
#196286=CARTESIAN_POINT('Ctrl Pts',(-16.6916475320491,19.7683953861157,
5.65317541318284));
#196287=CARTESIAN_POINT('Ctrl Pts',(-16.6879315188447,19.7545963349029,
5.65401695884199));
#196288=CARTESIAN_POINT('Ctrl Pts',(-16.6822397980225,19.7325750749912,
5.65536358780497));
#196289=CARTESIAN_POINT('Ctrl Pts',(-16.6801731154415,19.7243766749394,
5.65586572957054));
#196290=CARTESIAN_POINT('Ctrl Pts',(-16.6766148625333,19.7098958680802,
5.65675415501764));
#196291=CARTESIAN_POINT('Ctrl Pts',(-16.6751028112034,19.7036185700887,
5.65713977260974));
#196292=CARTESIAN_POINT('Ctrl Pts',(-16.6720348246296,19.6906208913539,
5.65793928666919));
#196293=CARTESIAN_POINT('Ctrl Pts',(-16.6704829736021,19.683899634042,5.65835330946692));
#196294=CARTESIAN_POINT('Ctrl Pts',(-16.6665839212048,19.6666276802532,
5.65941879883399));
#196295=CARTESIAN_POINT('Ctrl Pts',(-16.6642846438029,19.656066470778,5.66007179478921));
#196296=CARTESIAN_POINT('Ctrl Pts',(-16.6550256923499,19.6119135344231,
5.6628082424807));
#196297=CARTESIAN_POINT('Ctrl Pts',(-16.6488024887766,19.5781742867419,
5.66491503381012));
#196298=CARTESIAN_POINT('Ctrl Pts',(-16.634726328015,19.4898827353299,5.67047234159992));
#196299=CARTESIAN_POINT('Ctrl Pts',(-16.6281792838235,19.4351513336547,
5.67396129228824));
#196300=CARTESIAN_POINT('Ctrl Pts',(-16.6150299603028,19.2711853157515,
5.68453441106383));
#196301=CARTESIAN_POINT('Ctrl Pts',(-16.614751119347,19.1616338439582,5.69176695807165));
#196302=CARTESIAN_POINT('Ctrl Pts',(-16.6317988055526,18.9344877472608,
5.70681380616292));
#196303=CARTESIAN_POINT('Ctrl Pts',(-16.6505518532563,18.8173513797986,
5.71460005278452));
#196304=CARTESIAN_POINT('Ctrl Pts',(-16.681294158312,18.693140498366,5.72250355889524));
#196305=CARTESIAN_POINT('Ctrl Pts',(-16.6836451175635,18.683909305912,5.72308871218566));
#196306=CARTESIAN_POINT('Ctrl Pts',(-16.687220254165,18.670257263039,5.72395047294302));
#196307=CARTESIAN_POINT('Ctrl Pts',(-16.6883965816445,18.6658241648208,
5.72422973615586));
#196308=CARTESIAN_POINT('Ctrl Pts',(-16.6905147514381,18.6579450294181,
5.72472502739638));
#196309=CARTESIAN_POINT('Ctrl Pts',(-16.6914509166828,18.6544975251854,
5.72494137902286));
#196310=CARTESIAN_POINT('Ctrl Pts',(-16.6934819415484,18.6470922817078,
5.72540531467222));
#196311=CARTESIAN_POINT('Ctrl Pts',(-16.6945795875958,18.6431353649466,
5.72565273456437));
#196312=CARTESIAN_POINT('Ctrl Pts',(-16.6976400750763,18.6322259112284,
5.7263336254351));
#196313=CARTESIAN_POINT('Ctrl Pts',(-16.6996270233462,18.6252801139184,
5.72676571799974));
#196314=CARTESIAN_POINT('Ctrl Pts',(-16.7106873875433,18.5873516092909,
5.72911815673883));
#196315=CARTESIAN_POINT('Ctrl Pts',(-16.720433586824,18.5565675749139,5.73100165451978));
#196316=CARTESIAN_POINT('Ctrl Pts',(-16.7835874233358,18.3718847288774,
5.74221145155072));
#196317=CARTESIAN_POINT('Ctrl Pts',(-16.8539128066446,18.2243350421972,
5.75082103770599));
#196318=CARTESIAN_POINT('Ctrl Pts',(-17.0025823754461,17.9872561163335,
5.76614036298775));
#196319=CARTESIAN_POINT('Ctrl Pts',(-17.0727799955103,17.8935407360068,
5.7726664777862));
#196320=CARTESIAN_POINT('Ctrl Pts',(-17.1598309163756,17.7954135749015,
5.78035112157564));
#196321=CARTESIAN_POINT('Ctrl Pts',(-17.1694225770657,17.7848195403478,
5.78119268949349));
#196322=CARTESIAN_POINT('Ctrl Pts',(-17.1848584795014,17.7681136439012,
5.78253934742032));
#196323=CARTESIAN_POINT('Ctrl Pts',(-17.1906334541554,17.7619381693133,
5.78304149569069));
#196324=CARTESIAN_POINT('Ctrl Pts',(-17.2008835922263,17.7511079589549,
5.78392992871479));
#196325=CARTESIAN_POINT('Ctrl Pts',(-17.2053433731096,17.7464387664115,
5.78431554734269));
#196326=CARTESIAN_POINT('Ctrl Pts',(-17.214611700035,17.7368236953573,5.78511505968871));
#196327=CARTESIAN_POINT('Ctrl Pts',(-17.2194231934055,17.7318807761324,
5.78552907971818));
#196328=CARTESIAN_POINT('Ctrl Pts',(-17.2318355104677,17.7192534840602,
5.7865945538288));
#196329=CARTESIAN_POINT('Ctrl Pts',(-17.2394711123522,17.7116037152801,
5.78724753721127));
#196330=CARTESIAN_POINT('Ctrl Pts',(-17.2715836106546,17.679920637143,5.78998386305156));
#196331=CARTESIAN_POINT('Ctrl Pts',(-17.2965831283632,17.6564266720209,
5.79209054250307));
#196332=CARTESIAN_POINT('Ctrl Pts',(-17.3631987245203,17.5968039285216,
5.79764748483304));
#196333=CARTESIAN_POINT('Ctrl Pts',(-17.4056721213409,17.5616761021321,
5.8011361756376));
#196334=CARTESIAN_POINT('Ctrl Pts',(-17.5364174871662,17.4618711576012,
5.8117087952138));
#196335=CARTESIAN_POINT('Ctrl Pts',(-17.628378576334,17.4023393397481,5.81894110457133));
#196336=CARTESIAN_POINT('Ctrl Pts',(-17.8285948623188,17.2937232366365,
5.83398768012246));
#196337=CARTESIAN_POINT('Ctrl Pts',(-17.9372370829309,17.2460867622619,
5.84177389782223));
#196338=CARTESIAN_POINT('Ctrl Pts',(-18.0583237921455,17.2046995424321,
5.84967785102848));
#196339=CARTESIAN_POINT('Ctrl Pts',(-18.0673646321356,17.2016774380356,
5.85026342187156));
#196340=CARTESIAN_POINT('Ctrl Pts',(-18.0807866039397,17.1972914046923,
5.85112567708158));
#196341=CARTESIAN_POINT('Ctrl Pts',(-18.0851521077671,17.1958805342439,
5.85140502152598));
#196342=CARTESIAN_POINT('Ctrl Pts',(-18.0929251048228,17.1933962873606,
5.85190040193272));
#196343=CARTESIAN_POINT('Ctrl Pts',(-18.0963307563977,17.1923173357591,
5.85211676194425));
#196344=CARTESIAN_POINT('Ctrl Pts',(-18.1036560369449,17.1900169860328,
5.85258065435672));
#196345=CARTESIAN_POINT('Ctrl Pts',(-18.1075764809091,17.1887983706138,
5.85282802294923));
#196346=CARTESIAN_POINT('Ctrl Pts',(-18.1184015830366,17.1854680397902,
5.85350862797166));
#196347=CARTESIAN_POINT('Ctrl Pts',(-18.1253136125156,17.1833802087406,
5.85394048789924));
#196348=CARTESIAN_POINT('Ctrl Pts',(-18.1631336266428,17.1721672104047,
5.85628931374581));
#196349=CARTESIAN_POINT('Ctrl Pts',(-18.1942380155433,17.1637128156178,
5.8581695646932));
#196350=CARTESIAN_POINT('Ctrl Pts',(-18.3836984204913,17.1168347097578,
5.86937957679986));
#196351=CARTESIAN_POINT('Ctrl Pts',(-18.5458775879473,17.0960859650852,
5.87799163459532));
#196352=CARTESIAN_POINT('Ctrl Pts',(-18.8257594220325,17.0927601852233,
5.89331438631325));
#196353=CARTESIAN_POINT('Ctrl Pts',(-18.9425714843823,17.1010586806702,
5.89984131559868));
#196354=CARTESIAN_POINT('Ctrl Pts',(-19.0722154209582,17.1211426925299,
5.90752687623506));
#196355=CARTESIAN_POINT('Ctrl Pts',(-19.0863153124905,17.1234734391554,
5.90836845593411));
#196356=CARTESIAN_POINT('Ctrl Pts',(-19.1087177474292,17.1274100456412,
5.90971512919105));
#196357=CARTESIAN_POINT('Ctrl Pts',(-19.1170362866386,17.1289232271365,
5.91021728090427));
#196358=CARTESIAN_POINT('Ctrl Pts',(-19.1316910526064,17.1316797942373,
5.91110571793882));
#196359=CARTESIAN_POINT('Ctrl Pts',(-19.1380311090591,17.1329024197831,
5.91149133711498));
#196360=CARTESIAN_POINT('Ctrl Pts',(-19.1511326181378,17.1354911559339,
5.91229084855421));
#196361=CARTESIAN_POINT('Ctrl Pts',(-19.15789317787,17.1368613462658,5.91270486711858));
#196362=CARTESIAN_POINT('Ctrl Pts',(-19.1752291546862,17.1404631971072,
5.91377033315474));
#196363=CARTESIAN_POINT('Ctrl Pts',(-19.1857943003088,17.1427428296988,
5.91442330988309));
#196364=CARTESIAN_POINT('Ctrl Pts',(-19.2298156142123,17.1525946650549,
5.91715957123579));
#196365=CARTESIAN_POINT('Ctrl Pts',(-19.2631011747635,17.1608982032967,
5.91926619147819));
#196366=CARTESIAN_POINT('Ctrl Pts',(-19.3492893336922,17.1846377670335,
5.92482294039926));
#196367=CARTESIAN_POINT('Ctrl Pts',(-19.4018143762248,17.2013363461486,
5.92831149366923));
#196368=CARTESIAN_POINT('Ctrl Pts',(-19.6495380313013,17.2908761807727,
5.94524262438293));
#196369=CARTESIAN_POINT('Ctrl Pts',(-19.8338999692612,17.3902055265442,
5.9594330960303));
#196370=CARTESIAN_POINT('Ctrl Pts',(-20.0044081025877,17.5175500468468,
5.97284956146776));
#196371=CARTESIAN_POINT('Ctrl Pts',(-20.0080262622954,17.5202704016807,
5.9731343409666));
#196372=CARTESIAN_POINT('Ctrl Pts',(-20.0280040859915,17.5353915014961,
5.9747071046111));
#196373=CARTESIAN_POINT('Ctrl Pts',(-20.0441921156617,17.5480186089009,
5.9759827930487));
#196374=CARTESIAN_POINT('Ctrl Pts',(-20.0652189787214,17.5649178084252,
5.97763868684087));
#196375=CARTESIAN_POINT('Ctrl Pts',(-20.070224983017,17.5689788832143,5.97803283113335));
#196376=CARTESIAN_POINT('Ctrl Pts',(-20.0782557942458,17.575554852066,5.97866488456012));
#196377=CARTESIAN_POINT('Ctrl Pts',(-20.0812922316185,17.5780553850578,
5.97890380565795));
#196378=CARTESIAN_POINT('Ctrl Pts',(-20.0869640878364,17.5827527987693,
5.9793499572337));
#196379=CARTESIAN_POINT('Ctrl Pts',(-20.0896011359208,17.5849476233226,
5.97955733017561));
#196380=CARTESIAN_POINT('Ctrl Pts',(-20.0958375189305,17.5901639021519,
5.98004763376747));
#196381=CARTESIAN_POINT('Ctrl Pts',(-20.0994321731156,17.5931909674969,
5.98033015555393));
#196382=CARTESIAN_POINT('Ctrl Pts',(-20.1106650992561,17.6027143449578,
5.98121283432028));
#196383=CARTESIAN_POINT('Ctrl Pts',(-20.1182674443845,17.6092530802175,
5.98180997166686));
#196384=CARTESIAN_POINT('Ctrl Pts',(-20.136093300074,17.6248067104469,5.98321032302283));
#196385=CARTESIAN_POINT('Ctrl Pts',(-20.1462768884792,17.633866909768,5.98401047099876));
#196386=CARTESIAN_POINT('Ctrl Pts',(-20.1816927556655,17.6659940541057,
5.98679666377056));
#196387=CARTESIAN_POINT('Ctrl Pts',(-20.206454279316,17.6895742430562,5.98875100413453));
#196388=CARTESIAN_POINT('Ctrl Pts',(-20.284326861425,17.7674145850838,5.99496011804458));
#196389=CARTESIAN_POINT('Ctrl Pts',(-20.3350961644106,17.8239366791848,
5.99910812051783));
#196390=CARTESIAN_POINT('Ctrl Pts',(-20.4906344006038,18.0170482748422,
6.01259290952664));
#196391=CARTESIAN_POINT('Ctrl Pts',(-20.5818013932796,18.1636660924551,
6.02185812120613));
#196392=CARTESIAN_POINT('Ctrl Pts',(-20.6640047949979,18.3407643008365,
6.0332008999858));
#196393=CARTESIAN_POINT('Ctrl Pts',(-20.6734378025314,18.3619949186689,
6.03456168596892));
#196394=CARTESIAN_POINT('Ctrl Pts',(-20.6862667084011,18.392198690298,6.03650083631797));
#196395=CARTESIAN_POINT('Ctrl Pts',(-20.689954142672,18.4010467466129,6.03706928387687));
#196396=CARTESIAN_POINT('Ctrl Pts',(-20.6958419121568,18.4154492468315,
6.03799531862334));
#196397=CARTESIAN_POINT('Ctrl Pts',(-20.6980790756813,18.4209885617876,
6.03835165511188));
#196398=CARTESIAN_POINT('Ctrl Pts',(-20.7027082005255,18.4325916804175,
6.03909846932074));
#196399=CARTESIAN_POINT('Ctrl Pts',(-20.7050956580236,18.4386572028839,
6.03948909424094));
#196400=CARTESIAN_POINT('Ctrl Pts',(-20.7107003746611,18.4530916820114,
6.04041927369869));
#196401=CARTESIAN_POINT('Ctrl Pts',(-20.7138925354333,18.4614701914324,
6.04095966393404));
#196402=CARTESIAN_POINT('Ctrl Pts',(-20.7244298539957,18.489664697399,6.0427798374509));
#196403=CARTESIAN_POINT('Ctrl Pts',(-20.7315313067871,18.5095698537705,
6.04406770366818));
#196404=CARTESIAN_POINT('Ctrl Pts',(-20.7683470824126,18.6178596171728,
6.05109151753182));
#196405=CARTESIAN_POINT('Ctrl Pts',(-20.792491513349,18.7080166308508,6.05700840220353));
#196406=CARTESIAN_POINT('Ctrl Pts',(-20.8375614472673,18.9354384765633,
6.07205895999174));
#196407=CARTESIAN_POINT('Ctrl Pts',(-20.8510859071177,19.0737188231497,
6.08133524835691));
#196408=CARTESIAN_POINT('Ctrl Pts',(-20.85099958945,19.2123184341987,6.09037084431718));
#196409=CARTESIAN_POINT('Ctrl Pts',(-20.7225806064498,19.9371103026755,
6.13370788222325));
#196410=CARTESIAN_POINT('Ctrl Pts',(-20.7475746254701,19.8686597913444,
6.12932688331225));
#196411=CARTESIAN_POINT('Ctrl Pts',(-20.7690040796656,19.7989891620996,
6.12494588440125));
#196412=CARTESIAN_POINT('Ctrl Pts',(-20.7867733146095,19.7285043176892,
6.12056488549025));
#196413=CARTESIAN_POINT('Ctrl Pts',(-20.8045716231428,19.6579041476937,
6.11617671849557));
#196414=CARTESIAN_POINT('Ctrl Pts',(-20.8186976743736,19.5864875772687,
6.11178855150089));
#196415=CARTESIAN_POINT('Ctrl Pts',(-20.829107237801,19.5146686716041,6.10740038450622));
#196416=CARTESIAN_POINT('Ctrl Pts',(-20.8314491136676,19.4985113213839,
6.10641316324043));
#196417=CARTESIAN_POINT('Ctrl Pts',(-20.8336030954032,19.4823336157705,
6.10542594197464));
#196418=CARTESIAN_POINT('Ctrl Pts',(-20.8355690425741,19.4661402737596,
6.10443872070885));
#196419=CARTESIAN_POINT('Ctrl Pts',(-20.8457798800574,19.3820344615431,
6.09931124014673));
#196420=CARTESIAN_POINT('Ctrl Pts',(-20.8509432233709,19.2973036553198,
6.09418375958461));
#196421=CARTESIAN_POINT('Ctrl Pts',(-20.8509995343428,19.212404133962,6.0890562790225));
#196422=CARTESIAN_POINT('Origin',(-18.734,19.211,0.));
#196423=CARTESIAN_POINT('',(-20.7225806520317,19.9371101778417,7.1561613891005));
#196424=CARTESIAN_POINT('',(-20.7193263846487,19.9359291807798,6.93361859104258));
#196425=CARTESIAN_POINT('',(-20.7225806064498,19.9371103026755,0.));
#196426=CARTESIAN_POINT('Ctrl Pts',(-20.7225806520317,19.9371101778416,
7.15616138910049));
#196427=CARTESIAN_POINT('Ctrl Pts',(-20.7474159484405,19.8690943430094,
7.15141138139249));
#196428=CARTESIAN_POINT('Ctrl Pts',(-20.7687705059422,19.7997803889042,
7.14660726507682));
#196429=CARTESIAN_POINT('Ctrl Pts',(-20.804820214685,19.6570554559655,7.13689820720307));
#196430=CARTESIAN_POINT('Ctrl Pts',(-20.8192617654728,19.5837555936372,
7.13200643852526));
#196431=CARTESIAN_POINT('Ctrl Pts',(-20.8346727888099,19.4756767824713,
7.12505658086314));
#196432=CARTESIAN_POINT('Ctrl Pts',(-20.8387085624094,19.4413956374211,
7.12289062882407));
#196433=CARTESIAN_POINT('Ctrl Pts',(-20.8425871755636,19.3996888097489,
7.12031417054245));
#196434=CARTESIAN_POINT('Ctrl Pts',(-20.8432314558288,19.392345011776,7.11986270620306));
#196435=CARTESIAN_POINT('Ctrl Pts',(-20.8441775334979,19.3808732048737,
7.11916106506936));
#196436=CARTESIAN_POINT('Ctrl Pts',(-20.844505601465,19.3767475051867,7.11890945347458));
#196437=CARTESIAN_POINT('Ctrl Pts',(-20.8450939760417,19.3690631383027,
7.11844219556558));
#196438=CARTESIAN_POINT('Ctrl Pts',(-20.8453573820951,19.3655048112482,
7.11822638305092));
#196439=CARTESIAN_POINT('Ctrl Pts',(-20.8459354331692,19.3574183335078,
7.1177371868206));
#196440=CARTESIAN_POINT('Ctrl Pts',(-20.8462445117178,19.3528898370633,
7.11746411802914));
#196441=CARTESIAN_POINT('Ctrl Pts',(-20.847008104894,19.3411461236721,7.11675818511216));
#196442=CARTESIAN_POINT('Ctrl Pts',(-20.8474402335132,19.3339294415992,
7.11632654499942));
#196443=CARTESIAN_POINT('Ctrl Pts',(-20.8499256632896,19.288524865479,7.11362366095009));
#196444=CARTESIAN_POINT('Ctrl Pts',(-20.8509809805453,19.2502868206115,
7.11140442024796));
#196445=CARTESIAN_POINT('Ctrl Pts',(-20.8510792904772,19.0499008437116,
7.09997626877871));
#196446=CARTESIAN_POINT('Ctrl Pts',(-20.8325322788689,18.8882767547124,
7.09141462739975));
#196447=CARTESIAN_POINT('Ctrl Pts',(-20.7706268732764,18.6227424192177,
7.07645435582679));
#196448=CARTESIAN_POINT('Ctrl Pts',(-20.7371602945164,18.5172852286702,
7.07026709047522));
#196449=CARTESIAN_POINT('Ctrl Pts',(-20.6902873326397,18.4017842691172,
7.06296369090374));
#196450=CARTESIAN_POINT('Ctrl Pts',(-20.684821191827,18.3886941628057,7.06212824975919));
#196451=CARTESIAN_POINT('Ctrl Pts',(-20.6758998544184,18.3679193835598,
7.0607895662524));
#196452=CARTESIAN_POINT('Ctrl Pts',(-20.6725295629709,18.3601985538532,
7.0602892107299));
#196453=CARTESIAN_POINT('Ctrl Pts',(-20.6664968925576,18.3466005626899,
7.05940286367353));
#196454=CARTESIAN_POINT('Ctrl Pts',(-20.6638535463824,18.3407150380137,
7.05901752822334));
#196455=CARTESIAN_POINT('Ctrl Pts',(-20.6583232643876,18.3285507203292,
7.05821753221439));
#196456=CARTESIAN_POINT('Ctrl Pts',(-20.6554324090558,18.3222738032876,
7.05780274005969));
#196457=CARTESIAN_POINT('Ctrl Pts',(-20.6479172872326,18.3061642795821,
7.05673301278907));
#196458=CARTESIAN_POINT('Ctrl Pts',(-20.6432480026516,18.2963530075546,
7.05607652474451));
#196459=CARTESIAN_POINT('Ctrl Pts',(-20.6233051496814,18.2552665307349,
7.05330602627178));
#196460=CARTESIAN_POINT('Ctrl Pts',(-20.6073377264045,18.2243359488252,
7.05116794373237));
#196461=CARTESIAN_POINT('Ctrl Pts',(-20.5636050560382,18.1445129866121,
7.04550809799605));
#196462=CARTESIAN_POINT('Ctrl Pts',(-20.5346432954162,18.096310776336,7.04194610903537));
#196463=CARTESIAN_POINT('Ctrl Pts',(-20.434764503102,17.9441469727673,7.03023625290669));
#196464=CARTESIAN_POINT('Ctrl Pts',(-20.3564951910324,17.8453422172027,
7.02187677949724));
#196465=CARTESIAN_POINT('Ctrl Pts',(-20.2011017406371,17.6815219570291,
7.00699928978879));
#196466=CARTESIAN_POINT('Ctrl Pts',(-20.1272124737288,17.6139231839679,
7.00047974092646));
#196467=CARTESIAN_POINT('Ctrl Pts',(-20.0412146249944,17.5457754210711,
6.99370038661416));
#196468=CARTESIAN_POINT('Ctrl Pts',(-20.0335754797707,17.5398068469953,
6.99310475478002));
#196469=CARTESIAN_POINT('Ctrl Pts',(-20.0222359705239,17.531071899654,6.99223059639909));
#196470=CARTESIAN_POINT('Ctrl Pts',(-20.0185672438359,17.5282649242732,
6.99194930443228));
#196471=CARTESIAN_POINT('Ctrl Pts',(-20.0120424370305,17.5233065105439,
6.99145177832036));
#196472=CARTESIAN_POINT('Ctrl Pts',(-20.0091900673442,17.521150279454,6.99123520933562));
#196473=CARTESIAN_POINT('Ctrl Pts',(-20.0030671636771,17.51654604004,6.99077231698397));
#196474=CARTESIAN_POINT('Ctrl Pts',(-19.9997950121448,17.5141002751413,
6.99052614983439));
#196475=CARTESIAN_POINT('Ctrl Pts',(-19.990793867831,17.5074129063896,6.98985223138026));
#196476=CARTESIAN_POINT('Ctrl Pts',(-19.9850504388006,17.5031906972378,
6.98942581219983));
#196477=CARTESIAN_POINT('Ctrl Pts',(-19.9542778843873,17.4808071889138,
6.98715958004473));
#196478=CARTESIAN_POINT('Ctrl Pts',(-19.9288730018968,17.463165907458,6.98535350185525));
#196479=CARTESIAN_POINT('Ctrl Pts',(-19.8508165769635,17.4114608631174,
6.97996802680115));
#196480=CARTESIAN_POINT('Ctrl Pts',(-19.7970274258183,17.3791718932772,
6.97647537940241));
#196481=CARTESIAN_POINT('Ctrl Pts',(-19.6236648602482,17.285316648407,6.96564100763522));
#196482=CARTESIAN_POINT('Ctrl Pts',(-19.4996236656572,17.2327227096628,
6.95847225909595));
#196483=CARTESIAN_POINT('Ctrl Pts',(-19.3325234696925,17.1799600140554,
6.94874721448145));
#196484=CARTESIAN_POINT('Ctrl Pts',(-19.2932699637651,17.1688024996675,
6.94645998174456));
#196485=CARTESIAN_POINT('Ctrl Pts',(-19.2066104760124,17.1468561155067,
6.94137924087289));
#196486=CARTESIAN_POINT('Ctrl Pts',(-19.1591071501854,17.1365521178183,
6.93857393472468));
#196487=CARTESIAN_POINT('Ctrl Pts',(-19.0988926627521,17.1256460301408,
6.9349749174683));
#196488=CARTESIAN_POINT('Ctrl Pts',(-19.0864718544085,17.1235107386015,
6.93423027297472));
#196489=CARTESIAN_POINT('Ctrl Pts',(-19.0667599272158,17.1203029564151,
6.93304466656341));
#196490=CARTESIAN_POINT('Ctrl Pts',(-19.0594808772578,17.1191573927158,
6.93260602739138));
#196491=CARTESIAN_POINT('Ctrl Pts',(-19.0459068925946,17.1170937083349,
6.93178645097233));
#196492=CARTESIAN_POINT('Ctrl Pts',(-19.0396134965892,17.1161659117588,
6.93140582537003));
#196493=CARTESIAN_POINT('Ctrl Pts',(-19.0256263745375,17.1141682482353,
6.93055842098074));
#196494=CARTESIAN_POINT('Ctrl Pts',(-19.017930776983,17.1131123364422,6.93009120589956));
#196495=CARTESIAN_POINT('Ctrl Pts',(-18.995553342206,17.110167314363,6.92872969528718));
#196496=CARTESIAN_POINT('Ctrl Pts',(-18.980857510327,17.1083898421266,6.92783189143561));
#196497=CARTESIAN_POINT('Ctrl Pts',(-18.8639363752578,17.0954907962451,
6.92065851496285));
#196498=CARTESIAN_POINT('Ctrl Pts',(-18.7610577829605,17.0916781524953,
6.91415212142113));
#196499=CARTESIAN_POINT('Ctrl Pts',(-18.5026291718104,17.1009223459463,
6.8973658959693));
#196500=CARTESIAN_POINT('Ctrl Pts',(-18.3480384893603,17.123659548595,6.88689556588299));
#196501=CARTESIAN_POINT('Ctrl Pts',(-18.1465318942574,17.1764657291575,
6.87343968836));
#196502=CARTESIAN_POINT('Ctrl Pts',(-18.0962255101378,17.1916701186656,
6.87010195033607));
#196503=CARTESIAN_POINT('Ctrl Pts',(-18.0383148380403,17.2115534137393,
6.86632510580336));
#196504=CARTESIAN_POINT('Ctrl Pts',(-18.03011418316,17.2144256190468,6.86579183522964));
#196505=CARTESIAN_POINT('Ctrl Pts',(-18.017715663448,17.2188539742878,6.86498821128459));
#196506=CARTESIAN_POINT('Ctrl Pts',(-18.0135047835897,17.22037304285,6.86471573915166));
#196507=CARTESIAN_POINT('Ctrl Pts',(-18.0059505318238,17.2231253383946,
6.86422779793998));
#196508=CARTESIAN_POINT('Ctrl Pts',(-18.0026054427477,17.2243536548834,
6.86401204304164));
#196509=CARTESIAN_POINT('Ctrl Pts',(-17.9953385679417,17.2270428929411,
6.86354401496542));
#196510=CARTESIAN_POINT('Ctrl Pts',(-17.9914180204604,17.2285069941563,
6.86329193466112));
#196511=CARTESIAN_POINT('Ctrl Pts',(-17.9804047509988,17.2326570770059,
6.86258494077132));
#196512=CARTESIAN_POINT('Ctrl Pts',(-17.9733220014942,17.2353695925575,
6.86213158514618));
#196513=CARTESIAN_POINT('Ctrl Pts',(-17.9308014885549,17.2519164490607,
6.85941699620796));
#196514=CARTESIAN_POINT('Ctrl Pts',(-17.8957249109265,17.2666668265909,
6.85720729545368));
#196515=CARTESIAN_POINT('Ctrl Pts',(-17.7810018099989,17.3185924623995,
6.85001919777146));
#196516=CARTESIAN_POINT('Ctrl Pts',(-17.7032684351311,17.3597823663654,
6.84521015032519));
#196517=CARTESIAN_POINT('Ctrl Pts',(-17.4797361855879,17.4966873266967,
6.83095048302239));
#196518=CARTESIAN_POINT('Ctrl Pts',(-17.3429762592581,17.6056676806631,
6.8215775166648));
#196519=CARTESIAN_POINT('Ctrl Pts',(-17.2049682210269,17.746662712521,6.81011397695195));
#196520=CARTESIAN_POINT('Ctrl Pts',(-17.1890924168149,17.7634218948917,
6.80876166928866));
#196521=CARTESIAN_POINT('Ctrl Pts',(-17.1670331356938,17.7874848904002,
6.80683255740365));
#196522=CARTESIAN_POINT('Ctrl Pts',(-17.160619897499,17.7945765218028,6.80626552955011));
#196523=CARTESIAN_POINT('Ctrl Pts',(-17.1502810119813,17.8061659160412,
6.80534117894736));
#196524=CARTESIAN_POINT('Ctrl Pts',(-17.1463259169105,17.8106373179689,
6.80498509777216));
#196525=CARTESIAN_POINT('Ctrl Pts',(-17.1380892762196,17.8200289357792,
6.80423830760795));
#196526=CARTESIAN_POINT('Ctrl Pts',(-17.1338114564981,17.8249523227737,
6.80384744916028));
#196527=CARTESIAN_POINT('Ctrl Pts',(-17.1236935921876,17.8367063500857,
6.8029157725516));
#196528=CARTESIAN_POINT('Ctrl Pts',(-17.1178741922442,17.8435545228971,
6.80237411150478));
#196529=CARTESIAN_POINT('Ctrl Pts',(-17.098437849695,17.8667242602627,6.80054520621698));
#196530=CARTESIAN_POINT('Ctrl Pts',(-17.0850235049045,17.8832133910639,
6.79924977295498));
#196531=CARTESIAN_POINT('Ctrl Pts',(-17.0134819153951,17.973909939644,6.79215509273577));
#196532=CARTESIAN_POINT('Ctrl Pts',(-16.960119539907,18.051725096893,6.78617079542213));
#196533=CARTESIAN_POINT('Ctrl Pts',(-16.8276106994564,18.2756361114449,
6.76927204727213));
#196534=CARTESIAN_POINT('Ctrl Pts',(-16.7601866743178,18.427875982354,6.75808945758863));
#196535=CARTESIAN_POINT('Ctrl Pts',(-16.6988405050568,18.6265525091958,
6.74476051668973));
#196536=CARTESIAN_POINT('Ctrl Pts',(-16.6876451407811,18.667046533975,6.74210942100237));
#196537=CARTESIAN_POINT('Ctrl Pts',(-16.6758936051212,18.7150742148555,
6.73906264223644));
#196538=CARTESIAN_POINT('Ctrl Pts',(-16.6741639689389,18.7223080255509,
6.73860632595696));
#196539=CARTESIAN_POINT('Ctrl Pts',(-16.6714258940046,18.7340322496468,
6.73787109212545));
#196540=CARTESIAN_POINT('Ctrl Pts',(-16.6703939285332,18.7385170264142,
6.73759087448883));
#196541=CARTESIAN_POINT('Ctrl Pts',(-16.6685865293825,18.7464906159896,
6.73709453390167));
#196542=CARTESIAN_POINT('Ctrl Pts',(-16.6678052991537,18.7499780576742,
6.73687808206201));
#196543=CARTESIAN_POINT('Ctrl Pts',(-16.666147599959,18.7574669464904,6.73641464663031));
#196544=CARTESIAN_POINT('Ctrl Pts',(-16.665273914459,18.7614689525322,6.73616782341115));
#196545=CARTESIAN_POINT('Ctrl Pts',(-16.6629011176809,18.7724912199035,
6.73549025550176));
#196546=CARTESIAN_POINT('Ctrl Pts',(-16.6614260730888,18.7795166846653,
6.73506086707742));
#196547=CARTESIAN_POINT('Ctrl Pts',(-16.6536456238116,18.817534686077,6.73275000685802));
#196548=CARTESIAN_POINT('Ctrl Pts',(-16.6479992476788,18.8486598462564,
6.73090386350648));
#196549=CARTESIAN_POINT('Ctrl Pts',(-16.6174874829022,19.0413473482141,
6.71969127953706));
#196550=CARTESIAN_POINT('Ctrl Pts',(-16.6107039487309,19.2052275802291,
6.71105303120492));
#196551=CARTESIAN_POINT('Ctrl Pts',(-16.6315476577752,19.4850274368413,
6.69569421920797));
#196552=CARTESIAN_POINT('Ctrl Pts',(-16.6499147097709,19.6008462592448,
6.68915893316017));
#196553=CARTESIAN_POINT('Ctrl Pts',(-16.6811576349148,19.7284277916752,
6.68146396571602));
#196554=CARTESIAN_POINT('Ctrl Pts',(-16.6846978299566,19.7422757254214,
6.68062226628924));
#196555=CARTESIAN_POINT('Ctrl Pts',(-16.6905550866421,19.7642570689267,
6.6792754372436));
#196556=CARTESIAN_POINT('Ctrl Pts',(-16.6927811641099,19.7724144272182,
6.67877325054711));
#196557=CARTESIAN_POINT('Ctrl Pts',(-16.6967932165038,19.786777052302,6.67788477276624));
#196558=CARTESIAN_POINT('Ctrl Pts',(-16.6985588336342,19.7929879290143,
6.67749914802318));
#196559=CARTESIAN_POINT('Ctrl Pts',(-16.7022693161085,19.8058167849814,
6.67669964580785));
#196560=CARTESIAN_POINT('Ctrl Pts',(-16.7042181656882,19.8124335232657,
6.6762856421367));
#196561=CARTESIAN_POINT('Ctrl Pts',(-16.7093033174183,19.8293923824911,
6.67522025816239));
#196562=CARTESIAN_POINT('Ctrl Pts',(-16.7124865114523,19.8397201317102,
6.67456734905721));
#196563=CARTESIAN_POINT('Ctrl Pts',(-16.7260999404175,19.8827159645232,
6.6718317429244));
#196564=CARTESIAN_POINT('Ctrl Pts',(-16.7372436170309,19.9151510614031,
6.66972572425325));
#196565=CARTESIAN_POINT('Ctrl Pts',(-16.7683257312138,19.9989385695156,
6.66417094024307));
#196566=CARTESIAN_POINT('Ctrl Pts',(-16.7894882993709,20.0498062628873,
6.66068378418232));
#196567=CARTESIAN_POINT('Ctrl Pts',(-16.8585267617138,20.1990543854575,
6.65011411278765));
#196568=CARTESIAN_POINT('Ctrl Pts',(-16.9120656113153,20.2946064567013,
6.64288320705827));
#196569=CARTESIAN_POINT('Ctrl Pts',(-16.9983212096584,20.4239442703683,
6.63261379142985));
#196570=CARTESIAN_POINT('Ctrl Pts',(-17.0251487058255,20.4614567637566,
6.62957390294652));
#196571=CARTESIAN_POINT('Ctrl Pts',(-17.0664506570113,20.5153943539174,
6.62513730781065));
#196572=CARTESIAN_POINT('Ctrl Pts',(-17.0799886265947,20.5325187718193,
6.62371857433765));
#196573=CARTESIAN_POINT('Ctrl Pts',(-17.1264807415379,20.5894935841201,
6.61897107655121));
#196574=CARTESIAN_POINT('Ctrl Pts',(-17.1606320400863,20.6283485614777,
6.61568726421669));
#196575=CARTESIAN_POINT('Ctrl Pts',(-17.2021191079627,20.6721997602585,
6.61196390906098));
#196576=CARTESIAN_POINT('Ctrl Pts',(-17.2081017951444,20.6784462446857,
6.611433107483));
#196577=CARTESIAN_POINT('Ctrl Pts',(-17.2172328180984,20.68786366253,6.61063245937614));
#196578=CARTESIAN_POINT('Ctrl Pts',(-17.2203531029418,20.6910614965833,
6.61036051703167));
#196579=CARTESIAN_POINT('Ctrl Pts',(-17.2259798538746,20.6967916857548,
6.60987313972427));
#196580=CARTESIAN_POINT('Ctrl Pts',(-17.2284825974368,20.6993276002713,
6.60965742190244));
#196581=CARTESIAN_POINT('Ctrl Pts',(-17.2339436879374,20.7048332004119,
6.60918903127947));
#196582=CARTESIAN_POINT('Ctrl Pts',(-17.2369044465714,20.7078004124182,
6.60893655375838));
#196583=CARTESIAN_POINT('Ctrl Pts',(-17.2452688562879,20.7161334066703,
6.60822732145767));
#196584=CARTESIAN_POINT('Ctrl Pts',(-17.2506927376745,20.7214789173162,
6.60777214049947));
#196585=CARTESIAN_POINT('Ctrl Pts',(-17.2837779319999,20.7537359843825,
6.60502316864112));
#196586=CARTESIAN_POINT('Ctrl Pts',(-17.3121439347961,20.7799181356111,
6.60278244002634));
#196587=CARTESIAN_POINT('Ctrl Pts',(-17.409060098475,20.8645839310836,6.59544077474898));
#196588=CARTESIAN_POINT('Ctrl Pts',(-17.4806283980295,20.919469422023,6.59051754334627));
#196589=CARTESIAN_POINT('Ctrl Pts',(-17.6976390539644,21.0648956765038,
6.57631271833151));
#196590=CARTESIAN_POINT('Ctrl Pts',(-17.8508044851328,21.1425620640347,
6.56709216618477));
#196591=CARTESIAN_POINT('Ctrl Pts',(-18.033530476002,21.208892315459,6.55579961310107));
#196592=CARTESIAN_POINT('Ctrl Pts',(-18.0555482980019,21.2164761237761,
6.5544356318778));
#196593=CARTESIAN_POINT('Ctrl Pts',(-18.0868082411315,21.2266695881688,
6.5524926962936));
#196594=CARTESIAN_POINT('Ctrl Pts',(-18.0959503648643,21.2295821063095,
6.55192371190417));
#196595=CARTESIAN_POINT('Ctrl Pts',(-18.1108178102877,21.2342075196495,
6.55099704011313));
#196596=CARTESIAN_POINT('Ctrl Pts',(-18.1165312065234,21.2359585173766,
6.55064060686663));
#196597=CARTESIAN_POINT('Ctrl Pts',(-18.1284909605486,21.239568528711,6.54989378227633));
#196598=CARTESIAN_POINT('Ctrl Pts',(-18.1347386340321,21.2414229328685,
6.54950324458259));
#196599=CARTESIAN_POINT('Ctrl Pts',(-18.1495943130068,21.2457577848136,
6.54857362602149));
#196600=CARTESIAN_POINT('Ctrl Pts',(-18.1582096447353,21.2482124859175,
6.5480337121475));
#196601=CARTESIAN_POINT('Ctrl Pts',(-18.1871570075988,21.2562619470124,
6.54621680396353));
#196602=CARTESIAN_POINT('Ctrl Pts',(-18.2075564953543,21.2616074407743,
6.54493176620196));
#196603=CARTESIAN_POINT('Ctrl Pts',(-18.3182065143664,21.2888423594308,
6.53793434184216));
#196604=CARTESIAN_POINT('Ctrl Pts',(-18.4097320175698,21.3050772261686,
6.53204253693035));
#196605=CARTESIAN_POINT('Ctrl Pts',(-18.6540738514673,21.3320145923123,
6.51608767430365));
#196606=CARTESIAN_POINT('Ctrl Pts',(-18.8074878043951,21.3322465440226,
6.50581418189735));
#196607=CARTESIAN_POINT('Ctrl Pts',(-18.9637890465428,21.3154961144103,
6.49564082129242));
#196608=CARTESIAN_POINT('Ctrl Pts',(-18.9679946320586,21.31503265517,6.49536734032383));
#196609=CARTESIAN_POINT('Ctrl Pts',(-19.0233901029746,21.308759880766,6.49176863443538));
#196610=CARTESIAN_POINT('Ctrl Pts',(-19.0743574849866,21.3010959012391,
6.48849724382151));
#196611=CARTESIAN_POINT('Ctrl Pts',(-19.1334909402154,21.2899830820584,
6.48478614725468));
#196612=CARTESIAN_POINT('Ctrl Pts',(-19.141973591269,21.2883351249777,6.48425584852443));
#196613=CARTESIAN_POINT('Ctrl Pts',(-19.1548249262914,21.2857566911744,
6.48345580664324));
#196614=CARTESIAN_POINT('Ctrl Pts',(-19.1592010294498,21.2848642751063,
6.48318397233643));
#196615=CARTESIAN_POINT('Ctrl Pts',(-19.1670630405896,21.2832350486138,
6.48269670983927));
#196616=CARTESIAN_POINT('Ctrl Pts',(-19.1705499242318,21.2825032845863,
6.48248099939427));
#196617=CARTESIAN_POINT('Ctrl Pts',(-19.1781364844311,21.2808911480469,
6.48201253399976));
#196618=CARTESIAN_POINT('Ctrl Pts',(-19.1822353846312,21.2800074002357,
6.48175997482424));
#196619=CARTESIAN_POINT('Ctrl Pts',(-19.1937771523654,21.2774830164301,
6.48105028209307));
#196620=CARTESIAN_POINT('Ctrl Pts',(-19.2012139118971,21.2758143382789,
6.48059472563071));
#196621=CARTESIAN_POINT('Ctrl Pts',(-19.2463629007858,21.2654272837154,
6.47783860814311));
#196622=CARTESIAN_POINT('Ctrl Pts',(-19.2838417977379,21.2557155375536,
6.47559143028487));
#196623=CARTESIAN_POINT('Ctrl Pts',(-19.4080422008667,21.2198695309842,
6.46821752830712));
#196624=CARTESIAN_POINT('Ctrl Pts',(-19.493354889713,21.1891992921138,6.46327028952659));
#196625=CARTESIAN_POINT('Ctrl Pts',(-19.6380711399754,21.1264259320897,
6.45469347809467));
#196626=CARTESIAN_POINT('Ctrl Pts',(-19.6983881938933,21.096777397878,6.4510591451169));
#196627=CARTESIAN_POINT('Ctrl Pts',(-19.8577506079979,21.008795194398,6.44108688046683));
#196628=CARTESIAN_POINT('Ctrl Pts',(-19.953610171947,20.9451940339582,6.4346682451235));
#196629=CARTESIAN_POINT('Ctrl Pts',(-20.05503703672,20.8653136257788,6.42710452864922));
#196630=CARTESIAN_POINT('Ctrl Pts',(-20.0661522976138,20.8563761472563,
6.42626460005117));
#196631=CARTESIAN_POINT('Ctrl Pts',(-20.083705142669,20.8419679263199,6.42492007541292));
#196632=CARTESIAN_POINT('Ctrl Pts',(-20.0902018760824,20.8365696899818,
6.42441840637474));
#196633=CARTESIAN_POINT('Ctrl Pts',(-20.101606460532,20.8269774884282,6.42353053142399));
#196634=CARTESIAN_POINT('Ctrl Pts',(-20.106527787608,20.8227996602601,6.42314498895113));
#196635=CARTESIAN_POINT('Ctrl Pts',(-20.111652681476,20.8184085278175,6.42274095410773));
#196636=CARTESIAN_POINT('Ctrl Pts',(-20.1118754359795,20.81821758608,6.42272338760807));
#196637=CARTESIAN_POINT('Ctrl Pts',(-20.1122323321248,20.8179115314575,
6.42269523455801));
#196638=CARTESIAN_POINT('Ctrl Pts',(-20.1123664976654,20.8177964492612,
6.42268464934));
#196639=CARTESIAN_POINT('Ctrl Pts',(-20.1125825233666,20.8176111035055,
6.42266760267269));
#196640=CARTESIAN_POINT('Ctrl Pts',(-20.1126643933786,20.8175408497975,
6.42266114159677));
#196641=CARTESIAN_POINT('Ctrl Pts',(-20.1128530619556,20.8173789258285,
6.42264625054099));
#196642=CARTESIAN_POINT('Ctrl Pts',(-20.1129598580791,20.8172872500319,
6.42263782027382));
#196643=CARTESIAN_POINT('Ctrl Pts',(-20.1131635444003,20.8171123665886,
6.42262173947406));
#196644=CARTESIAN_POINT('Ctrl Pts',(-20.1132604385858,20.8170291587835,
6.42261408883189));
#196645=CARTESIAN_POINT('Ctrl Pts',(-20.1134453820028,20.8168703096903,
6.4225994841047));
#196646=CARTESIAN_POINT('Ctrl Pts',(-20.1135334334701,20.8167946691315,
6.42259253000973));
#196647=CARTESIAN_POINT('Ctrl Pts',(-20.1137016140503,20.816650169666,6.42257924599601));
#196648=CARTESIAN_POINT('Ctrl Pts',(-20.1137817453715,20.816581311022,6.42257291603884));
#196649=CARTESIAN_POINT('Ctrl Pts',(-20.1139349047252,20.8164496778142,
6.42256081599268));
#196650=CARTESIAN_POINT('Ctrl Pts',(-20.1140079293599,20.8163869079373,
6.42255504628345));
#196651=CARTESIAN_POINT('Ctrl Pts',(-20.1141475825316,20.8162668495155,
6.42254401118085));
#196652=CARTESIAN_POINT('Ctrl Pts',(-20.1142142117707,20.8162095618166,
6.42253874582322));
#196653=CARTESIAN_POINT('Ctrl Pts',(-20.1143417033352,20.8160999309942,
6.42252866996785));
#196654=CARTESIAN_POINT('Ctrl Pts',(-20.1144025662271,20.8160475885773,
6.42252385950047));
#196655=CARTESIAN_POINT('Ctrl Pts',(-20.1145190819811,20.8159473728678,
6.42251464962918));
#196656=CARTESIAN_POINT('Ctrl Pts',(-20.1145747354105,20.8158995000732,
6.42251025024249));
#196657=CARTESIAN_POINT('Ctrl Pts',(-20.1146813267376,20.8158078011132,
6.42250182362322));
#196658=CARTESIAN_POINT('Ctrl Pts',(-20.1147322651533,20.8157639753185,
6.42249779640108));
#196659=CARTESIAN_POINT('Ctrl Pts',(-20.1148298672938,20.8156799934502,
6.42249007940737));
#196660=CARTESIAN_POINT('Ctrl Pts',(-20.1148765312182,20.8156398378828,
6.4224863896627));
#196661=CARTESIAN_POINT('Ctrl Pts',(-20.1149659774766,20.8155628601704,
6.42247931666552));
#196662=CARTESIAN_POINT('Ctrl Pts',(-20.1150087600802,20.8155260383577,
6.42247593342723));
#196663=CARTESIAN_POINT('Ctrl Pts',(-20.1150907957113,20.81545542683,6.42246944570909));
#196664=CARTESIAN_POINT('Ctrl Pts',(-20.1151300489563,20.8154216373985,
6.42246634124169));
#196665=CARTESIAN_POINT('Ctrl Pts',(-20.1152263508583,20.815338733984,6.42245872451287));
#196666=CARTESIAN_POINT('Ctrl Pts',(-20.1152833981331,20.8152896184,6.4224542121849));
#196667=CARTESIAN_POINT('Ctrl Pts',(-20.1153964173092,20.8151923025939,
6.42244527192838));
#196668=CARTESIAN_POINT('Ctrl Pts',(-20.1154523954955,20.8151440971553,
6.42244084351495));
#196669=CARTESIAN_POINT('Ctrl Pts',(-20.1155633300425,20.8150485561047,
6.42243206688703));
#196670=CARTESIAN_POINT('Ctrl Pts',(-20.1156182802615,20.8150012259681,
6.4224277191703));
#196671=CARTESIAN_POINT('Ctrl Pts',(-20.1157271840613,20.8149074143782,
6.42241910197791));
#196672=CARTESIAN_POINT('Ctrl Pts',(-20.1157811377431,20.8148609330141,
6.42241483250535));
#196673=CARTESIAN_POINT('Ctrl Pts',(-20.1158880806818,20.814768791741,6.42240636928512));
#196674=CARTESIAN_POINT('Ctrl Pts',(-20.1159410700041,20.8147231319429,
6.4224021755428));
#196675=CARTESIAN_POINT('Ctrl Pts',(-20.1160461150854,20.8146326077067,
6.42239386137188));
#196676=CARTESIAN_POINT('Ctrl Pts',(-20.1160981709156,20.8145877433662,
6.42238974094765));
#196677=CARTESIAN_POINT('Ctrl Pts',(-20.1162013787273,20.8144987849092,
6.42238157109064));
#196678=CARTESIAN_POINT('Ctrl Pts',(-20.1162525307486,20.8144546909096,
6.42237752166424));
#196679=CARTESIAN_POINT('Ctrl Pts',(-20.1219737525498,20.8095224134375,
6.4219245736898));
#196680=CARTESIAN_POINT('Ctrl Pts',(-20.1276177980228,20.8046042403366,
6.42147443244445));
#196681=CARTESIAN_POINT('Ctrl Pts',(-20.143432311124,20.7906753435144,6.42020372841422));
#196682=CARTESIAN_POINT('Ctrl Pts',(-20.1535421456085,20.7815966108094,
6.41938032429356));
#196683=CARTESIAN_POINT('Ctrl Pts',(-20.17605592011,20.7609840613083,6.41752129041665));
#196684=CARTESIAN_POINT('Ctrl Pts',(-20.1884101370702,20.7493975409849,
6.41648345144874));
#196685=CARTESIAN_POINT('Ctrl Pts',(-20.2267855313752,20.7125313719577,
6.41320286292116));
#196686=CARTESIAN_POINT('Ctrl Pts',(-20.2522956523426,20.6867314009479,
6.41093806964548));
#196687=CARTESIAN_POINT('Ctrl Pts',(-20.3332489087791,20.6005365479115,
6.40346954403985));
#196688=CARTESIAN_POINT('Ctrl Pts',(-20.3858454393956,20.5375795423985,
6.39816081263688));
#196689=CARTESIAN_POINT('Ctrl Pts',(-20.4744527974017,20.4180537661683,
6.38839567876478));
#196690=CARTESIAN_POINT('Ctrl Pts',(-20.5116850375621,20.3625165480716,
6.38396924015682));
#196691=CARTESIAN_POINT('Ctrl Pts',(-20.5679592240902,20.2693241531686,
6.37678464319172));
#196692=CARTESIAN_POINT('Ctrl Pts',(-20.5886146683364,20.2326951918525,
6.3740185151432));
#196693=CARTESIAN_POINT('Ctrl Pts',(-20.6155608226734,20.1813971995547,
6.37024248010079));
#196694=CARTESIAN_POINT('Ctrl Pts',(-20.6227967858953,20.1672366726796,
6.36921014956012));
#196695=CARTESIAN_POINT('Ctrl Pts',(-20.6533657214605,20.1057132414828,
6.36477175695282));
#196696=CARTESIAN_POINT('Ctrl Pts',(-20.6750839771968,20.0575639723816,
6.36141656965233));
#196697=CARTESIAN_POINT('Ctrl Pts',(-20.6982561911844,20.0005962193275,
6.35762296356075));
#196698=CARTESIAN_POINT('Ctrl Pts',(-20.70148212357,19.9925233032807,6.35708941315014));
#196699=CARTESIAN_POINT('Ctrl Pts',(-20.7062940891013,19.9802626816277,
6.35628545200047));
#196700=CARTESIAN_POINT('Ctrl Pts',(-20.7079166710991,19.9760895527051,
6.3560129198921));
#196701=CARTESIAN_POINT('Ctrl Pts',(-20.7108068575052,19.9685858676909,
6.35552491474905));
#196702=CARTESIAN_POINT('Ctrl Pts',(-20.7120792971525,19.9652572462766,
6.35530915555972));
#196703=CARTESIAN_POINT('Ctrl Pts',(-20.7148275429871,19.9580132211009,
6.35484116809913));
#196704=CARTESIAN_POINT('Ctrl Pts',(-20.7163001432577,19.9540966628185,
6.35458913243066));
#196705=CARTESIAN_POINT('Ctrl Pts',(-20.7193819323901,19.9458259183912,
6.35405892678559));
#196706=CARTESIAN_POINT('Ctrl Pts',(-20.7209884312978,19.9414707539978,
6.35378091562846));
#196707=CARTESIAN_POINT('Ctrl Pts',(-20.7225806064498,19.9371103026756,
6.35350371400671));
#196708=CARTESIAN_POINT('',(-20.8509992748742,19.2092478064745,6.8890562790225));
#196709=CARTESIAN_POINT('Ctrl Pts',(-20.8509992748742,19.2092478064745,
6.8890562790225));
#196710=CARTESIAN_POINT('Ctrl Pts',(-20.8509006165464,19.0900488678703,
6.88186870628081));
#196711=CARTESIAN_POINT('Ctrl Pts',(-20.8407310772906,18.9712546433194,
6.87468113353913));
#196712=CARTESIAN_POINT('Ctrl Pts',(-20.8207141748805,18.8541905938,6.86749356079745));
#196713=CARTESIAN_POINT('Ctrl Pts',(-20.8084933107471,18.7827198030267,
6.86310535186655));
#196714=CARTESIAN_POINT('Ctrl Pts',(-20.7925724893354,18.7117380828087,
6.85871714293565));
#196715=CARTESIAN_POINT('Ctrl Pts',(-20.7730042905685,18.6416578330713,
6.85432893400475));
#196716=CARTESIAN_POINT('Ctrl Pts',(-20.7534651342531,18.5716815940441,
6.84994723790348));
#196717=CARTESIAN_POINT('Ctrl Pts',(-20.7302894754045,18.5026046302858,
6.84556554180221));
#196718=CARTESIAN_POINT('Ctrl Pts',(-20.7035811449958,18.4348304867639,
6.84118384570094));
#196719=CARTESIAN_POINT('Ctrl Pts',(-20.6769041990008,18.3671359832543,
6.8368072984413));
#196720=CARTESIAN_POINT('Ctrl Pts',(-20.6467030037516,18.3007417053632,
6.83243075118166));
#196721=CARTESIAN_POINT('Ctrl Pts',(-20.6131310722286,18.2360356860966,
6.82805420392202));
#196722=CARTESIAN_POINT('Ctrl Pts',(-20.5795804315366,18.171370702447,6.82368043220504));
#196723=CARTESIAN_POINT('Ctrl Pts',(-20.5426635175971,18.1083922801994,
6.81930666048806));
#196724=CARTESIAN_POINT('Ctrl Pts',(-20.5025812162806,18.0474668112085,
6.81493288877108));
#196725=CARTESIAN_POINT('Ctrl Pts',(-20.462511112143,17.9865598820423,6.81056044800752));
#196726=CARTESIAN_POINT('Ctrl Pts',(-20.419277797915,17.9277050686151,6.80618800724397));
#196727=CARTESIAN_POINT('Ctrl Pts',(-20.3731263263944,17.87124110896,6.80181556648041));
#196728=CARTESIAN_POINT('Ctrl Pts',(-20.3269736747756,17.8147757055152,
6.79744301391307));
#196729=CARTESIAN_POINT('Ctrl Pts',(-20.2779030245425,17.7607016494435,
6.79307046134572));
#196730=CARTESIAN_POINT('Ctrl Pts',(-20.2261996115099,17.709324495968,6.78869790877838));
#196731=CARTESIAN_POINT('Ctrl Pts',(-20.1744425387249,17.6578940213447,
6.78432081821105));
#196732=CARTESIAN_POINT('Ctrl Pts',(-20.120047590661,17.6091663783431,6.77994372764372));
#196733=CARTESIAN_POINT('Ctrl Pts',(-20.0633361651207,17.5634095290084,
6.77556663707639));
#196734=CARTESIAN_POINT('Ctrl Pts',(-20.006593767366,17.5176276901601,6.77118715601744));
#196735=CARTESIAN_POINT('Ctrl Pts',(-19.9475327641501,17.4748201585675,
6.76680767495849));
#196736=CARTESIAN_POINT('Ctrl Pts',(-19.8865046696903,17.4352122913079,
6.76242819389955));
#196737=CARTESIAN_POINT('Ctrl Pts',(-19.8253684033427,17.3955342193693,
6.75804095023982));
#196738=CARTESIAN_POINT('Ctrl Pts',(-19.7622585010731,17.3590673788382,
6.7536537065801));
#196739=CARTESIAN_POINT('Ctrl Pts',(-19.6975517419859,17.3259915012086,
6.74926646292037));
#196740=CARTESIAN_POINT('Ctrl Pts',(-19.6535573809355,17.3035030916047,
6.74628355998558));
#196741=CARTESIAN_POINT('Ctrl Pts',(-19.6088253272203,17.2825812380497,
6.74330065705079));
#196742=CARTESIAN_POINT('Ctrl Pts',(-19.5634785608967,17.2632694444527,
6.74031775411601));
#196743=CARTESIAN_POINT('Ctrl Pts',(-19.496768014386,17.2348594737004,6.73592954518511));
#196744=CARTESIAN_POINT('Ctrl Pts',(-19.4284659821156,17.2098253061038,
6.73154133625421));
#196745=CARTESIAN_POINT('Ctrl Pts',(-19.3589476876742,17.1883459545264,
6.72715312732332));
#196746=CARTESIAN_POINT('Ctrl Pts',(-19.2895325699082,17.1668984818681,
6.72277143122206));
#196747=CARTESIAN_POINT('Ctrl Pts',(-19.2189052304805,17.1489954929981,
6.71838973512079));
#196748=CARTESIAN_POINT('Ctrl Pts',(-19.1474611885827,17.1347681137369,
6.71400803901953));
#196749=CARTESIAN_POINT('Ctrl Pts',(-19.0761010991198,17.1205574527785,
6.70963149175989));
#196750=CARTESIAN_POINT('Ctrl Pts',(-19.0039266843584,17.1100139151849,
6.70525494450025));
#196751=CARTESIAN_POINT('Ctrl Pts',(-18.9313473123135,17.1032184557401,
6.70087839724061));
#196752=CARTESIAN_POINT('Ctrl Pts',(-18.8588139690515,17.0964273058769,
6.69650462552364));
#196753=CARTESIAN_POINT('Ctrl Pts',(-18.7858766571619,17.0933795627893,
6.69213085380667));
#196754=CARTESIAN_POINT('Ctrl Pts',(-18.7129521899235,17.0941046342129,
6.6877570820897));
#196755=CARTESIAN_POINT('Ctrl Pts',(-18.6400499138453,17.0948294849948,
6.68338464132615));
#196756=CARTESIAN_POINT('Ctrl Pts',(-18.5671609567223,17.0993248662018,
6.6790122005626));
#196757=CARTESIAN_POINT('Ctrl Pts',(-18.4947027860656,17.1075680796842,
6.67463975979905));
#196758=CARTESIAN_POINT('Ctrl Pts',(-18.4222427626455,17.1158115039466,
6.67026720723171));
#196759=CARTESIAN_POINT('Ctrl Pts',(-18.3502140266214,17.1278028942377,
6.66589465466437));
#196760=CARTESIAN_POINT('Ctrl Pts',(-18.2790278943175,17.1434678036241,
6.66152210209703));
#196761=CARTESIAN_POINT('Ctrl Pts',(-18.2077678823605,17.1591489706443,
6.6571450115297));
#196762=CARTESIAN_POINT('Ctrl Pts',(-18.1373526922077,17.1785111648149,
6.65276792096238));
#196763=CARTESIAN_POINT('Ctrl Pts',(-18.0681816040679,17.2014291842191,
6.64839083039505));
#196764=CARTESIAN_POINT('Ctrl Pts',(-17.9989727390297,17.2243597200042,
6.64401134933611));
#196765=CARTESIAN_POINT('Ctrl Pts',(-17.931009778539,17.2508497721603,6.63963186827717));
#196766=CARTESIAN_POINT('Ctrl Pts',(-17.8646724802128,17.2807257543705,
6.63525238721823));
#196767=CARTESIAN_POINT('Ctrl Pts',(-17.7982175994706,17.3106546915586,
6.63086514355852));
#196768=CARTESIAN_POINT('Ctrl Pts',(-17.733394564462,17.3439813228775,6.6264778998988));
#196769=CARTESIAN_POINT('Ctrl Pts',(-17.6705584443135,17.3804861219758,
6.62209065623908));
#196770=CARTESIAN_POINT('Ctrl Pts',(-17.6278359374864,17.4053058677688,
6.61910775330425));
#196771=CARTESIAN_POINT('Ctrl Pts',(-17.5860313573357,17.4315938434277,
6.61612485036941));
#196772=CARTESIAN_POINT('Ctrl Pts',(-17.545247850536,17.459270190028,6.61314194743458));
#196773=CARTESIAN_POINT('Ctrl Pts',(-17.485250407548,17.4999854241402,6.60875373850368));
#196774=CARTESIAN_POINT('Ctrl Pts',(-17.4272300397246,17.5438661041392,
6.60436552957278));
#196775=CARTESIAN_POINT('Ctrl Pts',(-17.3715403699668,17.590693622635,6.59997732064189));
#196776=CARTESIAN_POINT('Ctrl Pts',(-17.3159333529123,17.6374516413293,
6.59559562454062));
#196777=CARTESIAN_POINT('Ctrl Pts',(-17.2626505332032,17.687147508451,6.59121392843936));
#196778=CARTESIAN_POINT('Ctrl Pts',(-17.2120162539402,17.7395196308717,
6.58683223233809));
#196779=CARTESIAN_POINT('Ctrl Pts',(-17.161441473985,17.7918302118807,6.58245568507845));
#196780=CARTESIAN_POINT('Ctrl Pts',(-17.1135093856054,17.846810455921,6.57807913781881));
#196781=CARTESIAN_POINT('Ctrl Pts',(-17.0685096421059,17.9041599685647,
6.57370259055918));
#196782=CARTESIAN_POINT('Ctrl Pts',(-17.0235384367897,17.9614731109811,
6.5693288188422));
#196783=CARTESIAN_POINT('Ctrl Pts',(-16.9814961836085,18.021152162172,6.56495504712523));
#196784=CARTESIAN_POINT('Ctrl Pts',(-16.9426332229364,18.0828625659819,
6.56058127540825));
#196785=CARTESIAN_POINT('Ctrl Pts',(-16.9037820883938,18.1445541911087,
6.5562088346447));
#196786=CARTESIAN_POINT('Ctrl Pts',(-16.8681085825371,18.2082755337074,
6.55183639388115));
#196787=CARTESIAN_POINT('Ctrl Pts',(-16.8358195870604,18.2736632835888,
6.5474639531176));
#196788=CARTESIAN_POINT('Ctrl Pts',(-16.8035297659506,18.3390527054421,
6.54309140055025));
#196789=CARTESIAN_POINT('Ctrl Pts',(-16.77462483883,18.4061081857738,6.53871884798291));
#196790=CARTESIAN_POINT('Ctrl Pts',(-16.749264845334,18.474443575934,6.53434629541557));
#196791=CARTESIAN_POINT('Ctrl Pts',(-16.7238785322802,18.5428498871397,
6.52996920484824));
#196792=CARTESIAN_POINT('Ctrl Pts',(-16.702044666544,18.6125383070843,6.52559211428092));
#196793=CARTESIAN_POINT('Ctrl Pts',(-16.6838740959311,18.6831053348767,
6.52121502371359));
#196794=CARTESIAN_POINT('Ctrl Pts',(-16.6656936016952,18.753710901942,6.51683554265465));
#196795=CARTESIAN_POINT('Ctrl Pts',(-16.6511804819227,18.8251955591515,
6.51245606159571));
#196796=CARTESIAN_POINT('Ctrl Pts',(-16.6403943335872,18.8971460314664,
6.50807658053677));
#196797=CARTESIAN_POINT('Ctrl Pts',(-16.6295890668762,18.9692240355104,
6.50368933687705));
#196798=CARTESIAN_POINT('Ctrl Pts',(-16.6225240103776,19.0417690229283,
6.49930209321733));
#196799=CARTESIAN_POINT('Ctrl Pts',(-16.6192067693545,19.1143636113253,
6.49491484955761));
#196800=CARTESIAN_POINT('Ctrl Pts',(-16.6169513651074,19.1637209362375,
6.49193194662279));
#196801=CARTESIAN_POINT('Ctrl Pts',(-16.6164273661252,19.213101155059,6.48894904368797));
#196802=CARTESIAN_POINT('Ctrl Pts',(-16.6176234550289,19.2623743116388,
6.48596614075314));
#196803=CARTESIAN_POINT('Ctrl Pts',(-16.6193830456439,19.33486105039,6.48157793182225));
#196804=CARTESIAN_POINT('Ctrl Pts',(-16.6248744285954,19.4073987776277,
6.47718972289135));
#196805=CARTESIAN_POINT('Ctrl Pts',(-16.6341051990332,19.4795718244204,
6.47280151396045));
#196806=CARTESIAN_POINT('Ctrl Pts',(-16.6433222694771,19.5516377544453,
6.46841981785918));
#196807=CARTESIAN_POINT('Ctrl Pts',(-16.6562676494651,19.6233396039479,
6.46403812175792));
#196808=CARTESIAN_POINT('Ctrl Pts',(-16.6728969413429,19.6942630563101,
6.45965642565665));
#196809=CARTESIAN_POINT('Ctrl Pts',(-16.6895066924793,19.7651031679716,
6.45527987839701));
#196810=CARTESIAN_POINT('Ctrl Pts',(-16.709791646569,19.8351662321976,6.45090333113737));
#196811=CARTESIAN_POINT('Ctrl Pts',(-16.7336560032766,19.9040460985914,
6.44652678387773));
#196812=CARTESIAN_POINT('Ctrl Pts',(-16.7575052255561,19.9728822823751,
6.44215301216076));
#196813=CARTESIAN_POINT('Ctrl Pts',(-16.7849291889405,20.0405363024766,
6.43777924044378));
#196814=CARTESIAN_POINT('Ctrl Pts',(-16.8157820891441,20.1066165733569,
6.43340546872681));
#196815=CARTESIAN_POINT('Ctrl Pts',(-16.8466256007065,20.1726767357888,
6.42903302796326));
#196816=CARTESIAN_POINT('Ctrl Pts',(-16.8808957735922,20.2371636629374,
6.4246605871997));
#196817=CARTESIAN_POINT('Ctrl Pts',(-16.9183991025644,20.299706747123,6.42028814643615));
#196818=CARTESIAN_POINT('Ctrl Pts',(-16.9559033905009,20.3622514305421,
6.41591559386881));
#196819=CARTESIAN_POINT('Ctrl Pts',(-16.9966407488749,20.4228517596424,
6.41154304130146));
#196820=CARTESIAN_POINT('Ctrl Pts',(-17.0403731142006,20.4811641514771,
6.40717048873412));
#196821=CARTESIAN_POINT('Ctrl Pts',(-17.0841508666247,20.5395370621115,
6.40279339816679));
#196822=CARTESIAN_POINT('Ctrl Pts',(-17.1309295419556,20.5956169078821,
6.39841630759946));
#196823=CARTESIAN_POINT('Ctrl Pts',(-17.1804298596141,20.6490920759469,
6.39403921703214));
#196824=CARTESIAN_POINT('Ctrl Pts',(-17.2299572112332,20.7025964487856,
6.3896597359732));
#196825=CARTESIAN_POINT('Ctrl Pts',(-17.2822088187844,20.7534929748971,
6.38528025491425));
#196826=CARTESIAN_POINT('Ctrl Pts',(-17.3368694420736,20.8015078447176,
6.38090077385531));
#196827=CARTESIAN_POINT('Ctrl Pts',(-17.3916269509507,20.8496078205726,
6.37651353019559));
#196828=CARTESIAN_POINT('Ctrl Pts',(-17.4488016237927,20.8948156407834,
6.37212628653587));
#196829=CARTESIAN_POINT('Ctrl Pts',(-17.5080466246426,20.936898989353,6.36773904287615));
#196830=CARTESIAN_POINT('Ctrl Pts',(-17.5483275163857,20.9655116112385,
6.36475613994134));
#196831=CARTESIAN_POINT('Ctrl Pts',(-17.5895648351149,20.992680787336,6.36177323700652));
#196832=CARTESIAN_POINT('Ctrl Pts',(-17.6316431823902,21.0183456909703,
6.35879033407171));
#196833=CARTESIAN_POINT('Ctrl Pts',(-17.6935454914314,21.0561018505907,
6.35440212514081));
#196834=CARTESIAN_POINT('Ctrl Pts',(-17.7575106221335,21.0907477625256,
6.35001391620991));
#196835=CARTESIAN_POINT('Ctrl Pts',(-17.8231931738165,21.1220520467474,
6.34562570727901));
#196836=CARTESIAN_POINT('Ctrl Pts',(-17.8887782417024,21.1533098702211,
6.34124401117774));
#196837=CARTESIAN_POINT('Ctrl Pts',(-17.9560752387294,21.1812357055046,
6.33686231507648));
#196838=CARTESIAN_POINT('Ctrl Pts',(-18.0247117585804,21.2056426222719,
6.33248061897521));
#196839=CARTESIAN_POINT('Ctrl Pts',(-18.0932676250583,21.2300208589697,
6.32810407171557));
#196840=CARTESIAN_POINT('Ctrl Pts',(-18.1631594352662,21.2508882305582,
6.32372752445593));
#196841=CARTESIAN_POINT('Ctrl Pts',(-18.2339938260908,21.2681054484524,
6.31935097719629));
#196842=CARTESIAN_POINT('Ctrl Pts',(-18.3047832947742,21.2853117474373,
6.31497720547931));
#196843=CARTESIAN_POINT('Ctrl Pts',(-18.3765136904421,21.2988723720882,
6.31060343376233));
#196844=CARTESIAN_POINT('Ctrl Pts',(-18.4487768305315,21.3086979629104,
6.30622966204536));
#196845=CARTESIAN_POINT('Ctrl Pts',(-18.5210179807047,21.3185205637723,
6.3018572212818));
#196846=CARTESIAN_POINT('Ctrl Pts',(-18.593791075757,21.324610322322,6.29748478051825));
#196847=CARTESIAN_POINT('Ctrl Pts',(-18.6666797525652,21.3269293429331,
6.2931123397547));
#196848=CARTESIAN_POINT('Ctrl Pts',(-18.739570293145,21.3292484228418,6.28873978718735));
#196849=CARTESIAN_POINT('Ctrl Pts',(-18.8125759391511,21.3277965600418,
6.28436723462));
#196850=CARTESIAN_POINT('Ctrl Pts',(-18.885278932449,21.3225879533179,6.27999468205265));
#196851=CARTESIAN_POINT('Ctrl Pts',(-18.9580573796556,21.3173739409053,
6.27561759148533));
#196852=CARTESIAN_POINT('Ctrl Pts',(-19.0305320648495,21.3083954347151,
6.271240500918));
#196853=CARTESIAN_POINT('Ctrl Pts',(-19.1022898016639,21.2957185953961,
6.26686341035067));
#196854=CARTESIAN_POINT('Ctrl Pts',(-19.1740867280417,21.2830348327846,
6.26248392929173));
#196855=CARTESIAN_POINT('Ctrl Pts',(-19.2451654560889,21.2666488240854,
6.25810444823278));
#196856=CARTESIAN_POINT('Ctrl Pts',(-19.3151251217559,21.2466774284901,
6.25372496717384));
#196857=CARTESIAN_POINT('Ctrl Pts',(-19.3852087904606,21.2266706337303,
6.24933772351412));
#196858=CARTESIAN_POINT('Ctrl Pts',(-19.4541689789711,21.2030659176042,
6.2449504798544));
#196859=CARTESIAN_POINT('Ctrl Pts',(-19.5216226105736,21.176029166021,6.24056323619467));
#196860=CARTESIAN_POINT('Ctrl Pts',(-19.5674845802465,21.1576467801997,
6.23758033325987));
#196861=CARTESIAN_POINT('Ctrl Pts',(-19.6126505362295,21.1376788808132,
6.23459743032507));
#196862=CARTESIAN_POINT('Ctrl Pts',(-19.6570068699279,21.1161895753614,
6.23161452739027));
#196863=CARTESIAN_POINT('Ctrl Pts',(-19.7222419452859,21.0845851494847,
6.22722755755952));
#196864=CARTESIAN_POINT('Ctrl Pts',(-19.7859792078907,21.0495646312771,
6.22284058772878));
#196865=CARTESIAN_POINT('Ctrl Pts',(-19.8478374654086,21.0112930596579,
6.21845361789804));
#196866=CARTESIAN_POINT('Ctrl Pts',(-19.909611732559,20.9730734526993,6.21407260463999));
#196867=CARTESIAN_POINT('Ctrl Pts',(-19.9695116495685,20.9316118007376,
6.20969159138194));
#196868=CARTESIAN_POINT('Ctrl Pts',(-20.0271786199974,20.8871199410489,
6.2053105781239));
#196869=CARTESIAN_POINT('Ctrl Pts',(-20.0847863205701,20.842673809896,6.20093406765183));
#196870=CARTESIAN_POINT('Ctrl Pts',(-20.1401652493039,20.7952039448503,
6.19655755717977));
#196871=CARTESIAN_POINT('Ctrl Pts',(-20.1929853613383,20.744965682602,6.19218104670771));
#196872=CARTESIAN_POINT('Ctrl Pts',(-20.2457686121849,20.6947624797648,
6.18780759043921));
#196873=CARTESIAN_POINT('Ctrl Pts',(-20.2959962435443,20.6417950475088,
6.18343413417072));
#196874=CARTESIAN_POINT('Ctrl Pts',(-20.3433722233214,20.5863581521922,
6.17906067790223));
#196875=CARTESIAN_POINT('Ctrl Pts',(-20.3907430256954,20.5309273152021,
6.17468769957944));
#196876=CARTESIAN_POINT('Ctrl Pts',(-20.4352624726779,20.4730279095114,
6.17031472125665));
#196877=CARTESIAN_POINT('Ctrl Pts',(-20.4766732169317,20.4129896251586,
6.16594174293386));
#196878=CARTESIAN_POINT('Ctrl Pts',(-20.5180810237668,20.3529555995455,
6.16156907480276));
#196879=CARTESIAN_POINT('Ctrl Pts',(-20.5563802984135,20.2907833982918,
6.15719640667166));
#196880=CARTESIAN_POINT('Ctrl Pts',(-20.5913568209819,20.2268319937627,
6.15282373854055));
#196881=CARTESIAN_POINT('Ctrl Pts',(-20.6263573794093,20.1628366418419,
6.14844806551282));
#196882=CARTESIAN_POINT('Ctrl Pts',(-20.6580304038045,20.097060073715,6.1440723924851));
#196883=CARTESIAN_POINT('Ctrl Pts',(-20.6862080123007,20.029885142562,6.13969671945737));
#196884=CARTESIAN_POINT('Ctrl Pts',(-20.699063262214,19.999238449178,6.13770044037933));
#196885=CARTESIAN_POINT('Ctrl Pts',(-20.7111916428231,19.9683009800593,
6.13570416130129));
#196886=CARTESIAN_POINT('Ctrl Pts',(-20.7225806064498,19.9371103026755,
6.13370788222325));
#196887=CARTESIAN_POINT('Ctrl Pts',(-20.7193263846487,19.9359291807798,
6.93361859104258));
#196888=CARTESIAN_POINT('Ctrl Pts',(-20.8041092873412,19.7029525977831,
6.91876474293293));
#196889=CARTESIAN_POINT('Ctrl Pts',(-20.8501557633723,19.455755786691,6.90391089482328));
#196890=CARTESIAN_POINT('Ctrl Pts',(-20.8523540255571,19.2092594247491,
6.88905704671363));
#196891=CARTESIAN_POINT('Origin',(-18.734,19.211,0.));
#196892=CARTESIAN_POINT('',(-20.7225806376299,19.9371102172836,7.95734465602265));
#196893=CARTESIAN_POINT('',(-20.7225805951215,19.9371103337003,7.73405229189664));
#196894=CARTESIAN_POINT('',(-20.7225806064498,19.9371103026755,0.));
#196895=CARTESIAN_POINT('',(-20.8509992001742,19.2090893169909,7.9107295377978));
#196896=CARTESIAN_POINT('Ctrl Pts',(-20.7225806376299,19.9371102172836,
7.95734465602265));
#196897=CARTESIAN_POINT('Ctrl Pts',(-20.7291121252103,19.919222588893,7.95624414180481));
#196898=CARTESIAN_POINT('Ctrl Pts',(-20.7354039661561,19.9012421605658,
7.95513590187344));
#196899=CARTESIAN_POINT('Ctrl Pts',(-20.7459519908274,19.8697403662776,
7.95318939765545));
#196900=CARTESIAN_POINT('Ctrl Pts',(-20.750314926476,19.8562625715911,7.95235506982288));
#196901=CARTESIAN_POINT('Ctrl Pts',(-20.7570544827814,19.8347070115582,
7.95101783580892));
#196902=CARTESIAN_POINT('Ctrl Pts',(-20.7595187944765,19.8266569553473,
7.95051780654351));
#196903=CARTESIAN_POINT('Ctrl Pts',(-20.7637864744158,19.8124129061224,
7.94963183860058));
#196904=CARTESIAN_POINT('Ctrl Pts',(-20.7656096801624,19.8062249334664,
7.94924655418107));
#196905=CARTESIAN_POINT('Ctrl Pts',(-20.7693280068598,19.7933887822314,
7.94844646764524));
#196906=CARTESIAN_POINT('Ctrl Pts',(-20.7712189012909,19.7867394685418,
7.94803153296288));
#196907=CARTESIAN_POINT('Ctrl Pts',(-20.776000877776,19.7696051452156,7.94696102106728));
#196908=CARTESIAN_POINT('Ctrl Pts',(-20.7788437604023,19.7591069984308,
7.94630388655289));
#196909=CARTESIAN_POINT('Ctrl Pts',(-20.7848190493571,19.7363478502189,
7.94487644813674));
#196910=CARTESIAN_POINT('Ctrl Pts',(-20.7879226517855,19.7240797857062,
7.94410523988962));
#196911=CARTESIAN_POINT('Ctrl Pts',(-20.79663369605,19.6883001750311,7.9418506504463));
#196912=CARTESIAN_POINT('Ctrl Pts',(-20.8019485508008,19.6647201088789,
7.94035804879104));
#196913=CARTESIAN_POINT('Ctrl Pts',(-20.8363441701446,19.4989337435183,
7.92981464048068));
#196914=CARTESIAN_POINT('Ctrl Pts',(-20.8511300496375,19.354183419222,7.92031689761982));
#196915=CARTESIAN_POINT('Ctrl Pts',(-20.8509991383138,19.2090899270172,
7.9107294698959));
#196916=CARTESIAN_POINT('Ctrl Pts',(-20.8509991377698,19.2090893241665,
7.91072943006099));
#196917=CARTESIAN_POINT('Ctrl Pts',(-20.8508884781824,19.0864802207074,
7.90262771640683));
#196918=CARTESIAN_POINT('Ctrl Pts',(-20.8401264233866,18.9640980462868,
7.89450602327149));
#196919=CARTESIAN_POINT('Ctrl Pts',(-20.8166444877547,18.8309488995711,
7.88604140362766));
#196920=CARTESIAN_POINT('Ctrl Pts',(-20.8143518770747,18.8185933419533,
7.88525966249503));
#196921=CARTESIAN_POINT('Ctrl Pts',(-20.8106712447903,18.79969691162,7.88407055609758));
#196922=CARTESIAN_POINT('Ctrl Pts',(-20.8093620685976,18.7931412004733,
7.88365922007583));
#196923=CARTESIAN_POINT('Ctrl Pts',(-20.8071513246146,18.7823376149929,
7.88298345591827));
#196924=CARTESIAN_POINT('Ctrl Pts',(-20.8062677126641,18.7780861715292,
7.88271806667172));
#196925=CARTESIAN_POINT('Ctrl Pts',(-20.8045210245981,18.7698099847755,
7.88220252958522));
#196926=CARTESIAN_POINT('Ctrl Pts',(-20.8036592792767,18.7657849831742,
7.8819523088479));
#196927=CARTESIAN_POINT('Ctrl Pts',(-20.8020280139237,18.758272835495,7.88148627742611));
#196928=CARTESIAN_POINT('Ctrl Pts',(-20.8012614185466,18.7547851608302,
7.88127030886671));
#196929=CARTESIAN_POINT('Ctrl Pts',(-20.7994932703637,18.7468368285063,
7.88077900949322));
#196930=CARTESIAN_POINT('Ctrl Pts',(-20.798486093141,18.7423774740627,7.8805040045889));
#196931=CARTESIAN_POINT('Ctrl Pts',(-20.7953527020585,18.7287103144358,
7.87966301332656));
#196932=CARTESIAN_POINT('Ctrl Pts',(-20.7931792402859,18.7195133094844,
7.87909966895684));
#196933=CARTESIAN_POINT('Ctrl Pts',(-20.7619486492839,18.5912058239648,
7.87127265776304));
#196934=CARTESIAN_POINT('Ctrl Pts',(-20.7226547857507,18.4748060396478,
7.86455352025937));
#196935=CARTESIAN_POINT('Ctrl Pts',(-20.6449226699513,18.2971368669933,
7.85400321025685));
#196936=CARTESIAN_POINT('Ctrl Pts',(-20.6130669211926,18.2333095354677,
7.85014917507173));
#196937=CARTESIAN_POINT('Ctrl Pts',(-20.5342699927172,18.093564082889,7.841359277442));
#196938=CARTESIAN_POINT('Ctrl Pts',(-20.4856310622552,18.0187661967483,
7.8364009271598));
#196939=CARTESIAN_POINT('Ctrl Pts',(-20.4120571944111,17.9198852277896,
7.82930999235392));
#196940=CARTESIAN_POINT('Ctrl Pts',(-20.3910302400536,17.8930076279039,
7.82732377723733));
#196941=CARTESIAN_POINT('Ctrl Pts',(-20.362452302932,17.8582433502222,7.82466997628898));
#196942=CARTESIAN_POINT('Ctrl Pts',(-20.3554761973758,17.8498892803699,
7.82402559363929));
#196943=CARTESIAN_POINT('Ctrl Pts',(-20.3439632617759,17.8363163608519,
7.82296752082302));
#196944=CARTESIAN_POINT('Ctrl Pts',(-20.3394646764143,17.8310652250735,
7.82255540289719));
#196945=CARTESIAN_POINT('Ctrl Pts',(-20.3307199814935,17.820958307142,7.82175677518002));
#196946=CARTESIAN_POINT('Ctrl Pts',(-20.3264772410794,17.8160997016274,
7.82137040766717));
#196947=CARTESIAN_POINT('Ctrl Pts',(-20.3166485638874,17.8049476064496,
7.820477854729));
#196948=CARTESIAN_POINT('Ctrl Pts',(-20.3110472026305,17.7986679116916,
7.8199710262088));
#196949=CARTESIAN_POINT('Ctrl Pts',(-20.2959250278497,17.7819165499962,
7.81860752145994));
#196950=CARTESIAN_POINT('Ctrl Pts',(-20.2863365214536,17.7715068223187,
7.81774798835765));
#196951=CARTESIAN_POINT('Ctrl Pts',(-20.2021785208533,17.6819597386844,
7.810245842946));
#196952=CARTESIAN_POINT('Ctrl Pts',(-20.121730411581,17.6085923620633,7.80334364909822));
#196953=CARTESIAN_POINT('Ctrl Pts',(-19.9589817777189,17.4816495084809,
7.78990413415877));
#196954=CARTESIAN_POINT('Ctrl Pts',(-19.8778834651647,17.4269701061156,
7.78341902518482));
#196955=CARTESIAN_POINT('Ctrl Pts',(-19.7310607048379,17.3421160455268,
7.77224181004057));
#196956=CARTESIAN_POINT('Ctrl Pts',(-19.6670207069335,17.3093346565223,
7.76753757203429));
#196957=CARTESIAN_POINT('Ctrl Pts',(-19.5707250730171,17.2660801092606,
7.76082224655149));
#196958=CARTESIAN_POINT('Ctrl Pts',(-19.5396905692237,17.2530201145167,
7.75871054995631));
#196959=CARTESIAN_POINT('Ctrl Pts',(-19.5015752441705,17.2380402126393,
7.75619162059581));
#196960=CARTESIAN_POINT('Ctrl Pts',(-19.4947808259641,17.2354103117293,
7.7557454429911));
#196961=CARTESIAN_POINT('Ctrl Pts',(-19.4840926732908,17.231336588093,7.75504818249384));
#196962=CARTESIAN_POINT('Ctrl Pts',(-19.4802081111425,17.2298690859721,
7.75479571859328));
#196963=CARTESIAN_POINT('Ctrl Pts',(-19.4729791093083,17.227162406764,7.75432769652576));
#196964=CARTESIAN_POINT('Ctrl Pts',(-19.4696358885392,17.2259202635427,
7.75411196708751));
#196965=CARTESIAN_POINT('Ctrl Pts',(-19.4620487625848,17.2231231358259,
7.75362400244998));
#196966=CARTESIAN_POINT('Ctrl Pts',(-19.4578030177817,17.2215732935993,
7.75335207568659));
#196967=CARTESIAN_POINT('Ctrl Pts',(-19.4451910887339,17.2170152266156,
7.75254760100316));
#196968=CARTESIAN_POINT('Ctrl Pts',(-19.436810762246,17.2140460496254,7.75201731924416));
#196969=CARTESIAN_POINT('Ctrl Pts',(-19.3737732032367,17.1921576173445,
7.74805873576126));
#196970=CARTESIAN_POINT('Ctrl Pts',(-19.3183746982198,17.1754308417801,
7.74474981606306));
#196971=CARTESIAN_POINT('Ctrl Pts',(-19.1043129817761,17.1202599492673,
7.7323629742475));
#196972=CARTESIAN_POINT('Ctrl Pts',(-18.9420847437622,17.097937580278,7.72375664881158));
#196973=CARTESIAN_POINT('Ctrl Pts',(-18.7188554461252,17.0932025716156,
7.71138884768571));
#196974=CARTESIAN_POINT('Ctrl Pts',(-18.6587933218688,17.0944843586101,
7.7080148190298));
#196975=CARTESIAN_POINT('Ctrl Pts',(-18.5747314139418,17.0998610731298,
7.70317775289833));
#196976=CARTESIAN_POINT('Ctrl Pts',(-18.5506218788211,17.1018185359142,
7.70177728718358));
#196977=CARTESIAN_POINT('Ctrl Pts',(-18.5085725004037,17.1059589473461,
7.69930876151794));
#196978=CARTESIAN_POINT('Ctrl Pts',(-18.4906169854242,17.1079593277413,
7.69824637307862));
#196979=CARTESIAN_POINT('Ctrl Pts',(-18.4642189510212,17.1112428595442,
7.6966713796779));
#196980=CARTESIAN_POINT('Ctrl Pts',(-18.4557547752273,17.1123477050929,
7.69616439461756));
#196981=CARTESIAN_POINT('Ctrl Pts',(-18.4409105262776,17.1143767345143,
7.69527168229698));
#196982=CARTESIAN_POINT('Ctrl Pts',(-18.4345275227525,17.1152789329362,
7.69488665477982));
#196983=CARTESIAN_POINT('Ctrl Pts',(-18.4221294422942,17.1170891231432,
7.6941364939277));
#196984=CARTESIAN_POINT('Ctrl Pts',(-18.4161139566688,17.1179939161013,
7.69377146551617));
#196985=CARTESIAN_POINT('Ctrl Pts',(-18.4017239139267,17.1202217989332,
7.69289569594962));
#196986=CARTESIAN_POINT('Ctrl Pts',(-18.3933532906341,17.1215692881651,
7.69238418490325));
#196987=CARTESIAN_POINT('Ctrl Pts',(-18.3630631698079,17.1266321977784,
7.69052555047807));
#196988=CARTESIAN_POINT('Ctrl Pts',(-18.3411950439062,17.1306424648036,
7.68916910549212));
#196989=CARTESIAN_POINT('Ctrl Pts',(-18.1386253576824,17.171098294024,7.67646388002575));
#196990=CARTESIAN_POINT('Ctrl Pts',(-17.9633777793561,17.2306504682647,
7.66432808122214));
#196991=CARTESIAN_POINT('Ctrl Pts',(-17.7254567075873,17.3479144450112,
7.64681365653401));
#196992=CARTESIAN_POINT('Ctrl Pts',(-17.6549258545252,17.3878576331209,
7.64149071346173));
#196993=CARTESIAN_POINT('Ctrl Pts',(-17.5563829640792,17.4513916650659,
7.63401506756869));
#196994=CARTESIAN_POINT('Ctrl Pts',(-17.5264201602187,17.4718178155546,
7.63173696514549));
#196995=CARTESIAN_POINT('Ctrl Pts',(-17.490924800733,17.4973754796636,7.62904595716123));
#196996=CARTESIAN_POINT('Ctrl Pts',(-17.4848778515958,17.5017783028714,
7.62858780101063));
#196997=CARTESIAN_POINT('Ctrl Pts',(-17.4755024628351,17.5086809131879,
7.62787806404683));
#196998=CARTESIAN_POINT('Ctrl Pts',(-17.4721579151976,17.5111585726648,
7.62762499516659));
#196999=CARTESIAN_POINT('Ctrl Pts',(-17.4659618997561,17.5157769794248,
7.62715642516368));
#197000=CARTESIAN_POINT('Ctrl Pts',(-17.4631085596196,17.5179150463709,
7.62694074918401));
#197001=CARTESIAN_POINT('Ctrl Pts',(-17.4566611315629,17.5227717208308,
7.62645363365325));
#197002=CARTESIAN_POINT('Ctrl Pts',(-17.4530703236504,17.5254945943378,
7.62618249803873));
#197003=CARTESIAN_POINT('Ctrl Pts',(-17.4422374838663,17.533763639891,7.62536491255871));
#197004=CARTESIAN_POINT('Ctrl Pts',(-17.4350224684698,17.5393452554135,
7.62482089516974));
#197005=CARTESIAN_POINT('Ctrl Pts',(-17.3795517396309,17.5828340261551,
7.62064045331588));
#197006=CARTESIAN_POINT('Ctrl Pts',(-17.3329239421351,17.6227802750898,
7.61713848545565));
#197007=CARTESIAN_POINT('Ctrl Pts',(-17.1808267450645,17.7650025452924,
7.60550154960405));
#197008=CARTESIAN_POINT('Ctrl Pts',(-17.084283840583,17.8761977818435,7.59771434168961));
#197009=CARTESIAN_POINT('Ctrl Pts',(-16.9468098732126,18.0724725975678,
7.58451605297771));
#197010=CARTESIAN_POINT('Ctrl Pts',(-16.8986515413068,18.1518558403687,
7.57930752797287));
#197011=CARTESIAN_POINT('Ctrl Pts',(-16.8461314348078,18.2528322508335,
7.57267773573088));
#197012=CARTESIAN_POINT('Ctrl Pts',(-16.8366866412711,18.2716730459892,
7.57144084183032));
#197013=CARTESIAN_POINT('Ctrl Pts',(-16.8236313699821,18.2987166511657,
7.56966429638799));
#197014=CARTESIAN_POINT('Ctrl Pts',(-16.8197890595803,18.3068066119795,
7.5691327109669));
#197015=CARTESIAN_POINT('Ctrl Pts',(-16.8132398647239,18.3208247530898,
7.56821124401));
#197016=CARTESIAN_POINT('Ctrl Pts',(-16.8105087868877,18.3267415428209,
7.56782220508813));
#197017=CARTESIAN_POINT('Ctrl Pts',(-16.8053256186095,18.3381083427666,
7.56707457790801));
#197018=CARTESIAN_POINT('Ctrl Pts',(-16.8028691982743,18.3435563187227,
7.56671614340484));
#197019=CARTESIAN_POINT('Ctrl Pts',(-16.7965280894982,18.3577803879535,
7.56577999846621));
#197020=CARTESIAN_POINT('Ctrl Pts',(-16.7926799869105,18.3665725535029,
7.56520104125838));
#197021=CARTESIAN_POINT('Ctrl Pts',(-16.7796942813231,18.3968003104181,
7.56320933573633));
#197022=CARTESIAN_POINT('Ctrl Pts',(-16.7708511295329,18.4183598415019,
7.56178664467392));
#197023=CARTESIAN_POINT('Ctrl Pts',(-16.7001114915971,18.5992724084999,
7.54982651489317));
#197024=CARTESIAN_POINT('Ctrl Pts',(-16.6573822139315,18.7654105610991,
7.53862576974281));
#197025=CARTESIAN_POINT('Ctrl Pts',(-16.6233196920247,19.0242948317757,
7.52137082320096));
#197026=CARTESIAN_POINT('Ctrl Pts',(-16.6172798314759,19.1144189239202,
7.51541615508234));
#197027=CARTESIAN_POINT('Ctrl Pts',(-16.6168937886914,19.2432832556249,
7.50718309105437));
#197028=CARTESIAN_POINT('Ctrl Pts',(-16.617835188313,19.2819072844477,7.50475216117236));
#197029=CARTESIAN_POINT('Ctrl Pts',(-16.620227030745,19.3280933502732,7.50190599293462));
#197030=CARTESIAN_POINT('Ctrl Pts',(-16.6206620214824,19.3356980787129,
7.50143933646228));
#197031=CARTESIAN_POINT('Ctrl Pts',(-16.6214000350863,19.3474842907115,
7.50071932659188));
#197032=CARTESIAN_POINT('Ctrl Pts',(-16.6216744442227,19.3516674108587,
7.5004644162781));
#197033=CARTESIAN_POINT('Ctrl Pts',(-16.6222050637877,19.3594043190833,
7.49999415175133));
#197034=CARTESIAN_POINT('Ctrl Pts',(-16.6224578180082,19.3629582459515,
7.49977861183135));
#197035=CARTESIAN_POINT('Ctrl Pts',(-16.623047714322,19.3709668867107,7.49929395951222));
#197036=CARTESIAN_POINT('Ctrl Pts',(-16.6233899845081,19.3754211683442,
7.49902513786399));
#197037=CARTESIAN_POINT('Ctrl Pts',(-16.6244361112424,19.3884935642485,
7.49823827140866));
#197038=CARTESIAN_POINT('Ctrl Pts',(-16.6251786804385,19.3971086082078,
7.49772234790087));
#197039=CARTESIAN_POINT('Ctrl Pts',(-16.6307250118559,19.4571531292284,
7.49414343353275));
#197040=CARTESIAN_POINT('Ctrl Pts',(-16.6373572613694,19.5084007390801,
7.49117542686747));
#197041=CARTESIAN_POINT('Ctrl Pts',(-16.649441741637,19.58083789402,7.48703950299129));
#197042=CARTESIAN_POINT('Ctrl Pts',(-16.6533563583955,19.6022611432054,
7.48582377498518));
#197043=CARTESIAN_POINT('Ctrl Pts',(-16.6665988012666,19.6689000647081,
7.48205532923447));
#197044=CARTESIAN_POINT('Ctrl Pts',(-16.6770756471482,19.7138743759228,
7.47953088263622));
#197045=CARTESIAN_POINT('Ctrl Pts',(-16.717294840193,19.8641062705399,7.47106357103666));
#197046=CARTESIAN_POINT('Ctrl Pts',(-16.7537170579818,19.9673901696016,
7.46517522828271));
#197047=CARTESIAN_POINT('Ctrl Pts',(-16.8202492903854,20.1177993306105,
7.45603030492175));
#197048=CARTESIAN_POINT('Ctrl Pts',(-16.844504154324,20.1673114598088,7.45292245199185));
#197049=CARTESIAN_POINT('Ctrl Pts',(-16.8869471168382,20.2460178037331,
7.44777793347763));
#197050=CARTESIAN_POINT('Ctrl Pts',(-16.9039633395199,20.2758153980377,
7.44578066574025));
#197051=CARTESIAN_POINT('Ctrl Pts',(-16.9272822633564,20.3144386524507,
7.44311984036657));
#197052=CARTESIAN_POINT('Ctrl Pts',(-16.9329397970283,20.3236490813987,
7.4424798150795));
#197053=CARTESIAN_POINT('Ctrl Pts',(-16.9423229770063,20.3386657443901,
7.44142708502273));
#197054=CARTESIAN_POINT('Ctrl Pts',(-16.9460069521331,20.3444978803873,
7.44101592167097));
#197055=CARTESIAN_POINT('Ctrl Pts',(-16.9531942096207,20.3557538719202,
7.440217850813));
#197056=CARTESIAN_POINT('Ctrl Pts',(-16.9566939348732,20.3611799162546,
7.43983107871379));
#197057=CARTESIAN_POINT('Ctrl Pts',(-16.9648334168325,20.3736736775419,
7.43893571141123));
#197058=CARTESIAN_POINT('Ctrl Pts',(-16.969490776145,20.3807297444866,7.43842646013092));
#197059=CARTESIAN_POINT('Ctrl Pts',(-16.9821331264652,20.3996360433032,
7.43705219308795));
#197060=CARTESIAN_POINT('Ctrl Pts',(-16.9901959320627,20.4114334812718,
7.43618424953288));
#197061=CARTESIAN_POINT('Ctrl Pts',(-17.0652574951864,20.5189108909993,
7.42817966372938));
#197062=CARTESIAN_POINT('Ctrl Pts',(-17.1399371159666,20.6089585720942,
7.42074147848734));
#197063=CARTESIAN_POINT('Ctrl Pts',(-17.335419970133,20.8085286160105,7.40249415789795));
#197064=CARTESIAN_POINT('Ctrl Pts',(-17.4621895539076,20.9111829371932,
7.3915453069707));
#197065=CARTESIAN_POINT('Ctrl Pts',(-17.6270395001458,21.0158254108335,
7.3791363212405));
#197066=CARTESIAN_POINT('Ctrl Pts',(-17.6550249419876,21.0326941039494,
7.37708849567842));
#197067=CARTESIAN_POINT('Ctrl Pts',(-17.6896861232336,21.0525075614244,
7.37463336584474));
#197068=CARTESIAN_POINT('Ctrl Pts',(-17.6959994512029,21.0560735584769,
7.37418940877789));
#197069=CARTESIAN_POINT('Ctrl Pts',(-17.7059218465245,21.061611039547,7.37349685855344));
#197070=CARTESIAN_POINT('Ctrl Pts',(-17.7095184795922,21.0636045245423,
7.37324688937465));
#197071=CARTESIAN_POINT('Ctrl Pts',(-17.716249764005,21.0673098375628,7.37278107694451));
#197072=CARTESIAN_POINT('Ctrl Pts',(-17.7193829044525,21.0690241940178,
7.37256507733113));
#197073=CARTESIAN_POINT('Ctrl Pts',(-17.7265418257936,21.0729178237728,
7.37207338465479));
#197074=CARTESIAN_POINT('Ctrl Pts',(-17.7305703380924,21.0750919692347,
7.37179801954381));
#197075=CARTESIAN_POINT('Ctrl Pts',(-17.7429638625097,21.0817288049946,
7.37095483077659));
#197076=CARTESIAN_POINT('Ctrl Pts',(-17.7513519592315,21.0861484536394,
7.37038966922786));
#197077=CARTESIAN_POINT('Ctrl Pts',(-17.8671858038654,21.1461900317482,
7.36265696430112));
#197078=CARTESIAN_POINT('Ctrl Pts',(-17.9791941460035,21.1925660476455,
7.35601946546277));
#197079=CARTESIAN_POINT('Ctrl Pts',(-18.2651921078252,21.2831834505258,
7.33969351215518));
#197080=CARTESIAN_POINT('Ctrl Pts',(-18.4419635784852,21.3153841835301,
7.33007482409207));
#197081=CARTESIAN_POINT('Ctrl Pts',(-18.6421236143948,21.3261144541572,
7.31840385987958));
#197082=CARTESIAN_POINT('Ctrl Pts',(-18.6635892547781,21.3269377829711,
7.31714350484512));
#197083=CARTESIAN_POINT('Ctrl Pts',(-18.6940855872039,21.3276429287101,
7.31533911515375));
#197084=CARTESIAN_POINT('Ctrl Pts',(-18.7031091637951,21.3277938492931,
7.31480350167427));
#197085=CARTESIAN_POINT('Ctrl Pts',(-18.7186621427026,21.3279545059231,
7.31387726708604));
#197086=CARTESIAN_POINT('Ctrl Pts',(-18.725191180662,21.3279917414208,7.3134875124314));
#197087=CARTESIAN_POINT('Ctrl Pts',(-18.7376819724583,21.3280051925979,
7.31274005361289));
#197088=CARTESIAN_POINT('Ctrl Pts',(-18.7436436668569,21.3279864290939,
7.31238251063461));
#197089=CARTESIAN_POINT('Ctrl Pts',(-18.7591228073831,21.3278723237761,
7.31145208466416));
#197090=CARTESIAN_POINT('Ctrl Pts',(-18.7686397536666,21.3277379794056,
7.31087798473954));
#197091=CARTESIAN_POINT('Ctrl Pts',(-18.8009696850212,21.3270635107853,
7.30892057196584));
#197092=CARTESIAN_POINT('Ctrl Pts',(-18.8237740957008,21.3262187282114,
7.30752777270334));
#197093=CARTESIAN_POINT('Ctrl Pts',(-19.0240757464297,21.3155537148001,
7.29518346973431));
#197094=CARTESIAN_POINT('Ctrl Pts',(-19.1996626688947,21.2837817598868,
7.2835074205324));
#197095=CARTESIAN_POINT('Ctrl Pts',(-19.4506665521142,21.204834478496,7.26612447551382));
#197096=CARTESIAN_POINT('Ctrl Pts',(-19.5305375913909,21.1742922897261,
7.2604981719138));
#197097=CARTESIAN_POINT('Ctrl Pts',(-19.6424270641354,21.1235505092953,
7.25265697583508));
#197098=CARTESIAN_POINT('Ctrl Pts',(-19.6760922453198,21.1071940250878,
7.25030385331795));
#197099=CARTESIAN_POINT('Ctrl Pts',(-19.7160080819044,21.0864749017882,
7.24753654948697));
#197100=CARTESIAN_POINT('Ctrl Pts',(-19.7226892725834,21.0829614062218,
7.24707413568986));
#197101=CARTESIAN_POINT('Ctrl Pts',(-19.7330383412919,21.0774481888547,
7.24635925167028));
#197102=CARTESIAN_POINT('Ctrl Pts',(-19.7367192565314,21.0754732613603,
7.24610525906218));
#197103=CARTESIAN_POINT('Ctrl Pts',(-19.7435300027832,21.0717930773486,
7.24563584392917));
#197104=CARTESIAN_POINT('Ctrl Pts',(-19.746661345274,21.0700908270737,7.24542024109249));
#197105=CARTESIAN_POINT('Ctrl Pts',(-19.7537247519062,21.0662278995091,
7.24493438344008));
#197106=CARTESIAN_POINT('Ctrl Pts',(-19.7576542443098,21.0640626318949,
7.24466442585344));
#197107=CARTESIAN_POINT('Ctrl Pts',(-19.7692143329098,21.0576446856342,
7.24387113874183));
#197108=CARTESIAN_POINT('Ctrl Pts',(-19.7768256316007,21.053357190685,7.24334998279018));
#197109=CARTESIAN_POINT('Ctrl Pts',(-19.8310962761209,21.0223420962979,
7.23964069520895));
#197110=CARTESIAN_POINT('Ctrl Pts',(-19.8767530674185,20.9938900408248,
7.23655559273803));
#197111=CARTESIAN_POINT('Ctrl Pts',(-20.0608280282725,20.8691994595296,
7.22405651303708));
#197112=CARTESIAN_POINT('Ctrl Pts',(-20.1885934818829,20.7583408221315,
7.21518664224068));
#197113=CARTESIAN_POINT('Ctrl Pts',(-20.3564535135819,20.5733266073679,
7.20134226267846));
#197114=CARTESIAN_POINT('Ctrl Pts',(-20.4075288840627,20.5100720445777,
7.19675115653915));
#197115=CARTESIAN_POINT('Ctrl Pts',(-20.4662740161408,20.4280871280923,
7.19086730588545));
#197116=CARTESIAN_POINT('Ctrl Pts',(-20.4774848024831,20.4119725432133,
7.18971402008575));
#197117=CARTESIAN_POINT('Ctrl Pts',(-20.4933402561387,20.3884916625691,
7.18803707213709));
#197118=CARTESIAN_POINT('Ctrl Pts',(-20.4981663232809,20.381248662739,7.18752027265259));
#197119=CARTESIAN_POINT('Ctrl Pts',(-20.5065035620197,20.3685672871109,
7.18661617200641));
#197120=CARTESIAN_POINT('Ctrl Pts',(-20.5100347313983,20.3631421496468,
7.18622962706426));
#197121=CARTESIAN_POINT('Ctrl Pts',(-20.5168105267371,20.3526269362594,
7.18548081979802));
#197122=CARTESIAN_POINT('Ctrl Pts',(-20.5200583767544,20.3475390048255,
7.18511868266969));
#197123=CARTESIAN_POINT('Ctrl Pts',(-20.5277198427574,20.3354229629952,
7.18425671472095));
#197124=CARTESIAN_POINT('Ctrl Pts',(-20.5321139541324,20.3283826913369,
7.18375616803042));
#197125=CARTESIAN_POINT('Ctrl Pts',(-20.5475456153652,20.3033312362296,
7.18197606998159));
#197126=CARTESIAN_POINT('Ctrl Pts',(-20.5583545735578,20.2851813477433,
7.18068818849549));
#197127=CARTESIAN_POINT('Ctrl Pts',(-20.6295618924453,20.1614377216284,
7.17191698304319));
#197128=CARTESIAN_POINT('Ctrl Pts',(-20.680959667771,20.0510965762493,7.16412183349376));
#197129=CARTESIAN_POINT('Ctrl Pts',(-20.7225806520317,19.9371101778416,
7.15616138910049));
#197130=CARTESIAN_POINT('',(-20.8478091512629,19.2105385443279,7.68893948891723));
#197131=CARTESIAN_POINT('Ctrl Pts',(-20.8476071281599,19.2105314192558,
7.68905589350251));
#197132=CARTESIAN_POINT('Ctrl Pts',(-20.8482399779405,18.8850442033519,
7.6695533959637));
#197133=CARTESIAN_POINT('Ctrl Pts',(-20.6243347262999,17.8528832328165,
7.6076589628644));
#197134=CARTESIAN_POINT('Ctrl Pts',(-19.0148744805716,16.7235434527702,
7.5033725942046));
#197135=CARTESIAN_POINT('Ctrl Pts',(-16.7944747214404,17.6284159605188,
7.37619678752319));
#197136=CARTESIAN_POINT('Ctrl Pts',(-16.3534690248723,19.9852110982479,
7.24902098084175));
#197137=CARTESIAN_POINT('Ctrl Pts',(-18.0964527455682,21.6317156062949,
7.12184517416031));
#197138=CARTESIAN_POINT('Ctrl Pts',(-20.0208839011405,21.1569084882251,
7.01671104422726));
#197139=CARTESIAN_POINT('Ctrl Pts',(-20.6031710288178,20.2551147363436,
6.95396884985468));
#197140=CARTESIAN_POINT('Ctrl Pts',(-20.7193263846487,19.9359291807798,
6.93361859104258));
#197141=CARTESIAN_POINT('Ctrl Pts',(-20.8509999712458,19.2106510800831,
7.68710095623848));
#197142=CARTESIAN_POINT('Ctrl Pts',(-20.8510014361103,19.219538844338,7.68762152174537));
#197143=CARTESIAN_POINT('Ctrl Pts',(-20.8509469309451,19.2284264498996,
7.68814377561739));
#197144=CARTESIAN_POINT('Ctrl Pts',(-20.8507292584609,19.245937586264,7.68917624627481));
#197145=CARTESIAN_POINT('Ctrl Pts',(-20.8505693533295,19.2545609662676,
7.68968635124469));
#197146=CARTESIAN_POINT('Ctrl Pts',(-20.8502036147335,19.2693940125878,
7.69056674046743));
#197147=CARTESIAN_POINT('Ctrl Pts',(-20.8500231310445,19.2756042362602,
7.6909362299724));
#197148=CARTESIAN_POINT('Ctrl Pts',(-20.8496088606952,19.2879820912782,
7.69167449272669));
#197149=CARTESIAN_POINT('Ctrl Pts',(-20.8493754334253,19.2941496737455,
7.69204325113524));
#197150=CARTESIAN_POINT('Ctrl Pts',(-20.848855723493,19.3064570441778,7.69278093717845));
#197151=CARTESIAN_POINT('Ctrl Pts',(-20.8485696657275,19.3125967815423,
7.69314985421297));
#197152=CARTESIAN_POINT('Ctrl Pts',(-20.8477228781319,19.3292146330669,
7.69415087300361));
#197153=CARTESIAN_POINT('Ctrl Pts',(-20.847110980948,19.339689863623,7.69478457423149));
#197154=CARTESIAN_POINT('Ctrl Pts',(-20.8445147256942,19.3791005136108,
7.69717913939528));
#197155=CARTESIAN_POINT('Ctrl Pts',(-20.8420137559092,19.4079976241779,
7.69895610657007));
#197156=CARTESIAN_POINT('Ctrl Pts',(-20.8205669688998,19.6078964006027,
7.71140145936347));
#197157=CARTESIAN_POINT('Ctrl Pts',(-20.7814483759014,19.7758905836106,
7.72271594700901));
#197158=CARTESIAN_POINT('Ctrl Pts',(-20.7225805951212,19.9371103337009,
7.73405229189668));
#197159=CARTESIAN_POINT('Origin',(-18.734,19.211,0.));
#197160=CARTESIAN_POINT('',(-20.7225807266241,19.9371099735572,8.75434675637709));
#197161=CARTESIAN_POINT('',(-20.7225805753213,19.9371103879265,8.53521114927007));
#197162=CARTESIAN_POINT('',(-20.7225806064498,19.9371103026755,0.));
#197163=CARTESIAN_POINT('Ctrl Pts',(-20.7225807266241,19.9371099735572,
8.75434675637709));
#197164=CARTESIAN_POINT('Ctrl Pts',(-20.7522189772263,19.855940376575,8.74958604064089));
#197165=CARTESIAN_POINT('Ctrl Pts',(-20.7768869137611,19.7729578191594,
8.74492442009262));
#197166=CARTESIAN_POINT('Ctrl Pts',(-20.8270296549,19.5564351630452,8.73282225603236));
#197167=CARTESIAN_POINT('Ctrl Pts',(-20.8448588521927,19.4216336957187,
8.72532554013257));
#197168=CARTESIAN_POINT('Ctrl Pts',(-20.8502665613375,19.2692153684893,
8.71640096977841));
#197169=CARTESIAN_POINT('Ctrl Pts',(-20.850663023119,19.2523619374726,8.7154084679584));
#197170=CARTESIAN_POINT('Ctrl Pts',(-20.850952894071,19.2273224522688,8.71392477790426));
#197171=CARTESIAN_POINT('Ctrl Pts',(-20.8510001744524,19.2191385907097,
8.71343840732951));
#197172=CARTESIAN_POINT('Ctrl Pts',(-20.8509998627484,19.2045564795729,
8.71256913422892));
#197173=CARTESIAN_POINT('Ctrl Pts',(-20.850970719493,19.198158300236,8.71218681454019));
#197174=CARTESIAN_POINT('Ctrl Pts',(-20.8508481156843,19.1846683309743,
8.71137877086441));
#197175=CARTESIAN_POINT('Ctrl Pts',(-20.8507480205187,19.1775766938449,
8.71095284353293));
#197176=CARTESIAN_POINT('Ctrl Pts',(-20.850388624328,19.1588005204232,8.70982205354763));
#197177=CARTESIAN_POINT('Ctrl Pts',(-20.8500681972138,19.1471175218895,
8.7091152843866));
#197178=CARTESIAN_POINT('Ctrl Pts',(-20.8481220038578,19.0926263275845,
8.7058036403396));
#197179=CARTESIAN_POINT('Ctrl Pts',(-20.8452939286764,19.0498736478181,
8.70316139690633));
#197180=CARTESIAN_POINT('Ctrl Pts',(-20.8339020509085,18.9320661419609,
8.69575361357748));
#197181=CARTESIAN_POINT('Ctrl Pts',(-20.8226163050611,18.8573438067687,
8.69090980039786));
#197182=CARTESIAN_POINT('Ctrl Pts',(-20.7814380041058,18.6576814010828,
8.67762194008139));
#197183=CARTESIAN_POINT('Ctrl Pts',(-20.7441346497488,18.5345972382031,
8.66904372550594));
#197184=CARTESIAN_POINT('Ctrl Pts',(-20.6896744297274,18.4002580836196,
8.65959209010676));
#197185=CARTESIAN_POINT('Ctrl Pts',(-20.6832526056217,18.3849375144138,
8.6585131754329));
#197186=CARTESIAN_POINT('Ctrl Pts',(-20.6554930393278,18.3208381981372,
8.65399898740556));
#197187=CARTESIAN_POINT('Ctrl Pts',(-20.6324975721535,18.2727934484049,
8.65061473408322));
#197188=CARTESIAN_POINT('Ctrl Pts',(-20.6036571480965,18.2179506167347,
8.64679238727182));
#197189=CARTESIAN_POINT('Ctrl Pts',(-20.5995537700675,18.210263238401,8.64625757047998));
#197190=CARTESIAN_POINT('Ctrl Pts',(-20.5932681260821,18.1986605697957,
8.64545208353504));
#197191=CARTESIAN_POINT('Ctrl Pts',(-20.59112075744,18.1947266215475,8.64517928019296));
#197192=CARTESIAN_POINT('Ctrl Pts',(-20.5872434530345,18.1876767839009,
8.64469098568992));
#197193=CARTESIAN_POINT('Ctrl Pts',(-20.5855181356665,18.1845584309354,
8.64447520685968));
#197194=CARTESIAN_POINT('Ctrl Pts',(-20.581751667315,18.1777912819227,8.64400740200665));
#197195=CARTESIAN_POINT('Ctrl Pts',(-20.579707586274,18.1741441827135,8.6437555673661));
#197196=CARTESIAN_POINT('Ctrl Pts',(-20.5739344716727,18.1639148215671,
8.6430499566995));
#197197=CARTESIAN_POINT('Ctrl Pts',(-20.5701808972544,18.1573463816715,
8.64259772886939));
#197198=CARTESIAN_POINT('Ctrl Pts',(-20.547508229109,18.1181602433038,8.63990409673108));
#197199=CARTESIAN_POINT('Ctrl Pts',(-20.5277543658324,18.0860304440255,
8.63771330417982));
#197200=CARTESIAN_POINT('Ctrl Pts',(-20.4598654099191,17.9819478666145,
8.63061757981418));
#197201=CARTESIAN_POINT('Ctrl Pts',(-20.4081740321556,17.9124145235897,
8.62587707032943));
#197202=CARTESIAN_POINT('Ctrl Pts',(-20.2388260349945,17.7115978620897,
8.61158242665742));
#197203=CARTESIAN_POINT('Ctrl Pts',(-20.1089429969067,17.5916688874991,
8.60211687861015));
#197204=CARTESIAN_POINT('Ctrl Pts',(-19.9470525525317,17.4758576359767,
8.59054987254004));
#197205=CARTESIAN_POINT('Ctrl Pts',(-19.9281749310122,17.4628118830596,
8.58920552810913));
#197206=CARTESIAN_POINT('Ctrl Pts',(-19.9011551756503,17.4447812186854,
8.58728583925829));
#197207=CARTESIAN_POINT('Ctrl Pts',(-19.8931852443964,17.4395402764492,
8.5867201401416));
#197208=CARTESIAN_POINT('Ctrl Pts',(-19.8801738369424,17.431109519426,8.58579736495819));
#197209=CARTESIAN_POINT('Ctrl Pts',(-19.8751537608159,17.4278868010182,
8.58544152194468));
#197210=CARTESIAN_POINT('Ctrl Pts',(-19.8646137051622,17.4211831836323,
8.58469474966484));
#197211=CARTESIAN_POINT('Ctrl Pts',(-19.8590911251408,17.4177065089332,
8.5843036688113));
#197212=CARTESIAN_POINT('Ctrl Pts',(-19.845908544811,17.4094924352094,8.58337057243101));
#197213=CARTESIAN_POINT('Ctrl Pts',(-19.8382342601107,17.4047783046091,
8.58282770719576));
#197214=CARTESIAN_POINT('Ctrl Pts',(-19.8122482811057,17.389043244018,8.5809905001653));
#197215=CARTESIAN_POINT('Ctrl Pts',(-19.7938003050354,17.3782509617353,
8.5796878678121));
#197216=CARTESIAN_POINT('Ctrl Pts',(-19.6922718200734,17.3209010946873,
8.57252540608278));
#197217=CARTESIAN_POINT('Ctrl Pts',(-19.60629607635,17.279716986503,8.56647654423669));
#197218=CARTESIAN_POINT('Ctrl Pts',(-19.3593928288266,17.1813027939518,
8.54920496637082));
#197219=CARTESIAN_POINT('Ctrl Pts',(-19.1938931216584,17.1375289722929,
8.53769538467965));
#197220=CARTESIAN_POINT('Ctrl Pts',(-18.9884969801305,17.1090309416229,
8.52446042131896));
#197221=CARTESIAN_POINT('Ctrl Pts',(-18.9519260576004,17.1049251566184,
8.52214609667416));
#197222=CARTESIAN_POINT('Ctrl Pts',(-18.9081484127797,17.1011629589259,
8.5194403182823));
#197223=CARTESIAN_POINT('Ctrl Pts',(-18.9010293781574,17.1005874337673,
8.51900234602093));
#197224=CARTESIAN_POINT('Ctrl Pts',(-18.8894079540945,17.0997070952935,
8.51829085213219));
#197225=CARTESIAN_POINT('Ctrl Pts',(-18.8849073291344,17.0993806354967,
8.51801616090054));
#197226=CARTESIAN_POINT('Ctrl Pts',(-18.8768482173678,17.0988219528371,
8.51752584193458));
#197227=CARTESIAN_POINT('Ctrl Pts',(-18.8732901690566,17.0985843293676,
8.5173099160037));
#197228=CARTESIAN_POINT('Ctrl Pts',(-18.865582191699,17.0980891135052,8.51684333475449));
#197229=CARTESIAN_POINT('Ctrl Pts',(-18.8614321122457,17.0978347568418,
8.51659286250341));
#197230=CARTESIAN_POINT('Ctrl Pts',(-18.8498344687612,17.0971582321789,
8.51589490737903));
#197231=CARTESIAN_POINT('Ctrl Pts',(-18.84238529839,17.0967631933984,8.51544891916857));
#197232=CARTESIAN_POINT('Ctrl Pts',(-18.7990572879299,17.0946950537844,
8.51286745236707));
#197233=CARTESIAN_POINT('Ctrl Pts',(-18.763140298489,17.0938957832013,8.51077780604867));
#197234=CARTESIAN_POINT('Ctrl Pts',(-18.6474876313785,17.0942662865556,
8.50416158025336));
#197235=CARTESIAN_POINT('Ctrl Pts',(-18.5678287752104,17.0990257784595,
8.49977504680067));
#197236=CARTESIAN_POINT('Ctrl Pts',(-18.303670200793,17.1298516104654,8.48527502577618));
#197237=CARTESIAN_POINT('Ctrl Pts',(-18.1223947764205,17.1757370078603,
8.47531877649175));
#197238=CARTESIAN_POINT('Ctrl Pts',(-17.928982359863,17.2529086555016,8.46320677996891));
#197239=CARTESIAN_POINT('Ctrl Pts',(-17.908633746059,17.2613986029627,8.46191426416473));
#197240=CARTESIAN_POINT('Ctrl Pts',(-17.8806755942569,17.2735795872288,
8.46011152509643));
#197241=CARTESIAN_POINT('Ctrl Pts',(-17.8729495613334,17.2770008955054,
8.45961048060932));
#197242=CARTESIAN_POINT('Ctrl Pts',(-17.8597038628253,17.282961572672,8.45874644290631));
#197243=CARTESIAN_POINT('Ctrl Pts',(-17.854174227724,17.2854786363202,8.45838421785751));
#197244=CARTESIAN_POINT('Ctrl Pts',(-17.8427963070774,17.2907170558703,
8.45763572271638));
#197245=CARTESIAN_POINT('Ctrl Pts',(-17.8369494767149,17.293441405057,8.45724935223141));
#197246=CARTESIAN_POINT('Ctrl Pts',(-17.8233713535461,17.2998438658396,
8.4563479868652));
#197247=CARTESIAN_POINT('Ctrl Pts',(-17.8156497815401,17.3035422222832,
8.45583229372291));
#197248=CARTESIAN_POINT('Ctrl Pts',(-17.7910027527337,17.3155316140947,
8.45417611930579));
#197249=CARTESIAN_POINT('Ctrl Pts',(-17.7741658616627,17.3240016955108,
8.45302941331345));
#197250=CARTESIAN_POINT('Ctrl Pts',(-17.6906059658894,17.367445581228,8.44725974889972));
#197251=CARTESIAN_POINT('Ctrl Pts',(-17.6256769756934,17.4057349475905,
8.44252039714175));
#197252=CARTESIAN_POINT('Ctrl Pts',(-17.471989834757,17.5077864351577,8.43066494321757));
#197253=CARTESIAN_POINT('Ctrl Pts',(-17.3858611623779,17.5751136019879,
8.42344900590162));
#197254=CARTESIAN_POINT('Ctrl Pts',(-17.2947692253699,17.6584189222742,
8.4152944800237));
#197255=CARTESIAN_POINT('Ctrl Pts',(-17.2843213512106,17.668169794222,8.41435092368692));
#197256=CARTESIAN_POINT('Ctrl Pts',(-17.1982981693816,17.7500995263564,
8.40651689939572));
#197257=CARTESIAN_POINT('Ctrl Pts',(-17.1280545891836,17.8276870070585,
8.39968927472637));
#197258=CARTESIAN_POINT('Ctrl Pts',(-17.0578713896505,17.917796338987,8.39263256760226));
#197259=CARTESIAN_POINT('Ctrl Pts',(-17.0519716884127,17.9254792516289,
8.39203740685896));
#197260=CARTESIAN_POINT('Ctrl Pts',(-17.0433375216818,17.9368843424134,
8.39116380536707));
#197261=CARTESIAN_POINT('Ctrl Pts',(-17.0405622653227,17.940575281961,8.39088260417272));
#197262=CARTESIAN_POINT('Ctrl Pts',(-17.0356596557997,17.9471400950401,
8.39038517840229));
#197263=CARTESIAN_POINT('Ctrl Pts',(-17.0335274861383,17.9500103036172,
8.39016861948917));
#197264=CARTESIAN_POINT('Ctrl Pts',(-17.0289742399249,17.9561721817755,
8.38970568205226));
#197265=CARTESIAN_POINT('Ctrl Pts',(-17.0265554252253,17.9594654536803,
8.38945946009394));
#197266=CARTESIAN_POINT('Ctrl Pts',(-17.0199406846569,17.9685264449346,
8.388785236927));
#197267=CARTESIAN_POINT('Ctrl Pts',(-17.0157643036456,17.974308459388,8.38835856985102));
#197268=CARTESIAN_POINT('Ctrl Pts',(-16.9936033866211,18.0053182423631,
8.38608865195067));
#197269=CARTESIAN_POINT('Ctrl Pts',(-16.9761440462928,18.0309188388782,
8.38427926604911));
#197270=CARTESIAN_POINT('Ctrl Pts',(-16.8700946452666,18.1939984183922,
8.37309073227626));
#197271=CARTESIAN_POINT('Ctrl Pts',(-16.7971150548607,18.3409859508417,
8.36444696119417));
#197272=CARTESIAN_POINT('Ctrl Pts',(-16.7019681138647,18.6056973860495,
8.34905212373271));
#197273=CARTESIAN_POINT('Ctrl Pts',(-16.6714655090452,18.7195826938641,
8.34248371027389));
#197274=CARTESIAN_POINT('Ctrl Pts',(-16.6480481134493,18.8494778762623,
8.3347514563089));
#197275=CARTESIAN_POINT('Ctrl Pts',(-16.6456535663897,18.8635770916592,
8.33390930298938));
#197276=CARTESIAN_POINT('Ctrl Pts',(-16.6420704779496,18.8860516789945,
8.33256188334131));
#197277=CARTESIAN_POINT('Ctrl Pts',(-16.6407889426206,18.8944119353988,
8.33205956402231));
#197278=CARTESIAN_POINT('Ctrl Pts',(-16.6386174080589,18.9091681082599,
8.33117093173656));
#197279=CARTESIAN_POINT('Ctrl Pts',(-16.6377065046466,18.9155608736227,
8.3307852858548));
#197280=CARTESIAN_POINT('Ctrl Pts',(-16.6358832135593,18.9287899410996,
8.32998581847218));
#197281=CARTESIAN_POINT('Ctrl Pts',(-16.6349749583236,18.935626726872,8.3295718711602));
#197282=CARTESIAN_POINT('Ctrl Pts',(-16.6327298227402,18.9531835015115,
8.32850679781504));
#197283=CARTESIAN_POINT('Ctrl Pts',(-16.6314415732576,18.9639094091344,
8.32785414470023));
#197284=CARTESIAN_POINT('Ctrl Pts',(-16.6264109047706,19.0086866375756,
8.3251210177569));
#197285=CARTESIAN_POINT('Ctrl Pts',(-16.6234133439509,19.0428148553765,
8.32301727512132));
#197286=CARTESIAN_POINT('Ctrl Pts',(-16.6177640404778,19.1318859648987,
8.31746992324235));
#197287=CARTESIAN_POINT('Ctrl Pts',(-16.6164232626926,19.1868833638701,
8.31398805123392));
#197288=CARTESIAN_POINT('Ctrl Pts',(-16.6188187798023,19.3511610559734,
8.30342853226656));
#197289=CARTESIAN_POINT('Ctrl Pts',(-16.6288746993541,19.4601600212713,
8.2962024614806));
#197290=CARTESIAN_POINT('Ctrl Pts',(-16.6538348611804,19.6061014651274,
8.28642180140493));
#197291=CARTESIAN_POINT('Ctrl Pts',(-16.6614195817952,19.6441312584114,
8.28386460186058));
#197292=CARTESIAN_POINT('Ctrl Pts',(-16.6765391024102,19.7103956554802,
8.27941247669198));
#197293=CARTESIAN_POINT('Ctrl Pts',(-16.6836219886273,19.7387229185453,
8.27751047142428));
#197294=CARTESIAN_POINT('Ctrl Pts',(-16.7049052557349,19.8169311006764,
8.27227724577364));
#197295=CARTESIAN_POINT('Ctrl Pts',(-16.7203568740495,19.8664542720522,
8.26898378640082));
#197296=CARTESIAN_POINT('Ctrl Pts',(-16.7404929734054,19.9235262454128,
8.26525091262465));
#197297=CARTESIAN_POINT('Ctrl Pts',(-16.7434228587391,19.931670913839,8.2647197207549));
#197298=CARTESIAN_POINT('Ctrl Pts',(-16.7479412427383,19.9439935788488,
8.26391860215429));
#197299=CARTESIAN_POINT('Ctrl Pts',(-16.7494931146006,19.9481847777726,
8.26364657598865));
#197300=CARTESIAN_POINT('Ctrl Pts',(-16.752306032159,19.9557084751685,8.26315910956213));
#197301=CARTESIAN_POINT('Ctrl Pts',(-16.7535622224513,19.9590427160238,
8.26294338597385));
#197302=CARTESIAN_POINT('Ctrl Pts',(-16.7563141961476,19.9662916140888,
8.26247505316576));
#197303=CARTESIAN_POINT('Ctrl Pts',(-16.757813182072,19.970204993673,8.26222263884353));
#197304=CARTESIAN_POINT('Ctrl Pts',(-16.7620670397321,19.9812125131534,
8.26151376283832));
#197305=CARTESIAN_POINT('Ctrl Pts',(-16.7648485905373,19.9882963693495,
8.2610588724472));
#197306=CARTESIAN_POINT('Ctrl Pts',(-16.7819343837916,20.031128887543,8.2583154128152));
#197307=CARTESIAN_POINT('Ctrl Pts',(-16.7971745171345,20.0664992874279,
8.25607965902514));
#197308=CARTESIAN_POINT('Ctrl Pts',(-16.8511153954923,20.1828470977651,
8.24876278512226));
#197309=CARTESIAN_POINT('Ctrl Pts',(-16.8939998397795,20.2617821768188,
8.24385800745585));
#197310=CARTESIAN_POINT('Ctrl Pts',(-17.0331143137692,20.4830581434268,
8.22964458679385));
#197311=CARTESIAN_POINT('Ctrl Pts',(-17.1417772167226,20.61668979378,8.22039953697715));
#197312=CARTESIAN_POINT('Ctrl Pts',(-17.2821225632538,20.7518704488831,
8.20907945685341));
#197313=CARTESIAN_POINT('Ctrl Pts',(-17.2991363799216,20.76772610319,8.20771724328775));
#197314=CARTESIAN_POINT('Ctrl Pts',(-17.3235298112837,20.7897193578265,
8.20577640190152));
#197315=CARTESIAN_POINT('Ctrl Pts',(-17.3306956155906,20.7960923519253,
8.20520771462507));
#197316=CARTESIAN_POINT('Ctrl Pts',(-17.342395822329,20.8063565465964,8.20428139542877));
#197317=CARTESIAN_POINT('Ctrl Pts',(-17.3469038845547,20.8102776692836,
8.20392501575092));
#197318=CARTESIAN_POINT('Ctrl Pts',(-17.3563643580573,20.818436319324,8.20317819700084));
#197319=CARTESIAN_POINT('Ctrl Pts',(-17.3613198544722,20.822670158324,8.2027876111085));
#197320=CARTESIAN_POINT('Ctrl Pts',(-17.3731357820508,20.8326713315079,
8.20185768248212));
#197321=CARTESIAN_POINT('Ctrl Pts',(-17.3800134008482,20.8384180816819,
8.20131750525384));
#197322=CARTESIAN_POINT('Ctrl Pts',(-17.4032144384937,20.8575553579756,
8.19949879234696));
#197323=CARTESIAN_POINT('Ctrl Pts',(-17.4197012313071,20.870744996537,8.19821219140667));
#197324=CARTESIAN_POINT('Ctrl Pts',(-17.5099226896532,20.9407360272897,
8.19120018920189));
#197325=CARTESIAN_POINT('Ctrl Pts',(-17.5871358780116,20.9928671966894,
8.18529453154263));
#197326=CARTESIAN_POINT('Ctrl Pts',(-17.7908374746254,21.1116611367534,
8.16998787943476));
#197327=CARTESIAN_POINT('Ctrl Pts',(-17.9211043921061,21.1709146918714,
8.1604250858041));
#197328=CARTESIAN_POINT('Ctrl Pts',(-18.0694780540287,21.221047752965,8.15023441275153));
#197329=CARTESIAN_POINT('Ctrl Pts',(-18.0826620844429,21.2253585376332,
8.14933502201538));
#197330=CARTESIAN_POINT('Ctrl Pts',(-18.1452850713814,21.2451552747318,
8.14509462323706));
#197331=CARTESIAN_POINT('Ctrl Pts',(-18.1952435944756,21.2589539651773,
8.1418043431698));
#197332=CARTESIAN_POINT('Ctrl Pts',(-18.2540821953621,21.2729027087739,
8.13807460621232));
#197333=CARTESIAN_POINT('Ctrl Pts',(-18.2625144527184,21.274847199825,8.13754354295905));
#197334=CARTESIAN_POINT('Ctrl Pts',(-18.2753191277537,21.2777174038476,
8.13674257940073));
#197335=CARTESIAN_POINT('Ctrl Pts',(-18.2796828262511,21.2786810383653,
8.1364705808534));
#197336=CARTESIAN_POINT('Ctrl Pts',(-18.2875311824239,21.2803881438492,
8.13598314379505));
#197337=CARTESIAN_POINT('Ctrl Pts',(-18.291014677566,21.2811366379184,8.13576742211088));
#197338=CARTESIAN_POINT('Ctrl Pts',(-18.2985997636358,21.2827464126165,
8.13529907027226));
#197339=CARTESIAN_POINT('Ctrl Pts',(-18.3027020142004,21.2836043067019,
8.13504663514132));
#197340=CARTESIAN_POINT('Ctrl Pts',(-18.3142620634424,21.2859860251302,
8.13433764182958));
#197341=CARTESIAN_POINT('Ctrl Pts',(-18.3217256590964,21.2874818351457,
8.13388265577327));
#197342=CARTESIAN_POINT('Ctrl Pts',(-18.3670193537988,21.2963054939349,
8.13113738295973));
#197343=CARTESIAN_POINT('Ctrl Pts',(-18.4050382575322,21.3026401196899,
8.12889999277953));
#197344=CARTESIAN_POINT('Ctrl Pts',(-18.5322115249753,21.3202756433572,
8.1215749713631));
#197345=CARTESIAN_POINT('Ctrl Pts',(-18.6219144331793,21.3269399137165,
8.11666412986314));
#197346=CARTESIAN_POINT('Ctrl Pts',(-18.7802711693372,21.328602455447,8.1080524359446));
#197347=CARTESIAN_POINT('Ctrl Pts',(-18.8487610398305,21.3259966753661,
8.10434710093293));
#197348=CARTESIAN_POINT('Ctrl Pts',(-19.0310225401261,21.3101819681524,
8.09432351852859));
#197349=CARTESIAN_POINT('Ctrl Pts',(-19.144037020099,21.2910605606187,8.0879268651006));
#197350=CARTESIAN_POINT('Ctrl Pts',(-19.2687608141137,21.2593952425081,
8.08038797141464));
#197351=CARTESIAN_POINT('Ctrl Pts',(-19.2825411921549,21.2557480880415,
8.07954850510587));
#197352=CARTESIAN_POINT('Ctrl Pts',(-19.3044246480172,21.2497192133218,
8.07820458210845));
#197353=CARTESIAN_POINT('Ctrl Pts',(-19.3125522702886,21.2474276508693,
8.07770304827235));
#197354=CARTESIAN_POINT('Ctrl Pts',(-19.3268682220086,21.2432986838705,
8.07681533070574));
#197355=CARTESIAN_POINT('Ctrl Pts',(-19.3330622999406,21.2414814770135,
8.07642980965722));
#197356=CARTESIAN_POINT('Ctrl Pts',(-19.3458621526463,21.2376626133774,
8.07563013415225));
#197357=CARTESIAN_POINT('Ctrl Pts',(-19.3524666353939,21.235656924383,8.07521585158188));
#197358=CARTESIAN_POINT('Ctrl Pts',(-19.3694062850543,21.2304219707778,
8.07414893078798));
#197359=CARTESIAN_POINT('Ctrl Pts',(-19.3797266046036,21.2271456763914,
8.07349475524054));
#197360=CARTESIAN_POINT('Ctrl Pts',(-19.4221500904483,21.2133187495646,
8.07078815670395));
#197361=CARTESIAN_POINT('Ctrl Pts',(-19.4540220945009,21.2020798322743,
8.06871317277053));
#197362=CARTESIAN_POINT('Ctrl Pts',(-19.5363378606131,21.1708182091661,
8.06324182460417));
#197363=CARTESIAN_POINT('Ctrl Pts',(-19.5863024304945,21.1496111617254,
8.05980816256132));
#197364=CARTESIAN_POINT('Ctrl Pts',(-19.7604204463906,21.0676752926659,
8.04744754443502));
#197365=CARTESIAN_POINT('Ctrl Pts',(-19.8793790981298,20.9967442980095,
8.03824118458765));
#197366=CARTESIAN_POINT('Ctrl Pts',(-20.0636019481919,20.8608738260176,
8.02319282210838));
#197367=CARTESIAN_POINT('Ctrl Pts',(-20.1331082337134,20.8023594796302,
8.01730392784608));
#197368=CARTESIAN_POINT('Ctrl Pts',(-20.2056248303938,20.7328747198928,
8.01109910231789));
#197369=CARTESIAN_POINT('Ctrl Pts',(-20.212553648507,20.7261440265151,8.01050562250322));
#197370=CARTESIAN_POINT('Ctrl Pts',(-20.2227227842827,20.7161294786751,
8.00963400844907));
#197371=CARTESIAN_POINT('Ctrl Pts',(-20.2259987142839,20.7128821902946,
8.00935313147938));
#197372=CARTESIAN_POINT('Ctrl Pts',(-20.2317947414299,20.7070991587303,
8.00885606385245));
#197373=CARTESIAN_POINT('Ctrl Pts',(-20.2343190520514,20.7045677162204,
8.00863954065362));
#197374=CARTESIAN_POINT('Ctrl Pts',(-20.2397172002792,20.6991268211573,
8.00817644098127));
#197375=CARTESIAN_POINT('Ctrl Pts',(-20.2425890157268,20.6962154407168,
8.00793002232114));
#197376=CARTESIAN_POINT('Ctrl Pts',(-20.2484661114418,20.6902227428497,
8.0074255841677));
#197377=CARTESIAN_POINT('Ctrl Pts',(-20.2514704690679,20.6871405427362,
8.00716763603248));
#197378=CARTESIAN_POINT('Ctrl Pts',(-20.2652694054864,20.6728974296868,
8.00598239252414));
#197379=CARTESIAN_POINT('Ctrl Pts',(-20.2759507162323,20.6616267981184,
8.00506353270242));
#197380=CARTESIAN_POINT('Ctrl Pts',(-20.341053716511,20.5914001931569,7.99944663224406));
#197381=CARTESIAN_POINT('Ctrl Pts',(-20.39221704071,20.5295011652345,7.99495937219235));
#197382=CARTESIAN_POINT('Ctrl Pts',(-20.4809424811497,20.4087975083693,
7.98672379063677));
#197383=CARTESIAN_POINT('Ctrl Pts',(-20.519351799775,20.3507571006085,7.98296163937517));
#197384=CARTESIAN_POINT('Ctrl Pts',(-20.6215884078398,20.1783793228182,
7.97206933466951));
#197385=CARTESIAN_POINT('Ctrl Pts',(-20.6777336515715,20.0599315824275,
7.96490108863878));
#197386=CARTESIAN_POINT('Ctrl Pts',(-20.7225806376299,19.9371102172836,
7.95734465602265));
#197387=CARTESIAN_POINT('Ctrl Pts',(-20.7225805951212,19.9371103337009,
7.73405229189668));
#197388=CARTESIAN_POINT('Ctrl Pts',(-20.7059081256316,19.9827708177362,
7.73726295928993));
#197389=CARTESIAN_POINT('Ctrl Pts',(-20.6876516167336,20.0278883447379,
7.7404696596753));
#197390=CARTESIAN_POINT('Ctrl Pts',(-20.6420223308054,20.1303280441212,
7.7477806534552));
#197391=CARTESIAN_POINT('Ctrl Pts',(-20.6136163554537,20.1870927986601,
7.75185458536201));
#197392=CARTESIAN_POINT('Ctrl Pts',(-20.576383744976,20.2538227232164,7.75660091562334));
#197393=CARTESIAN_POINT('Ctrl Pts',(-20.5699624506865,20.2650868060294,
7.75740054882405));
#197394=CARTESIAN_POINT('Ctrl Pts',(-20.56082238396,20.2807831524705,7.75851187618657));
#197395=CARTESIAN_POINT('Ctrl Pts',(-20.5581903057717,20.2852652118984,
7.75882887302775));
#197396=CARTESIAN_POINT('Ctrl Pts',(-20.5536739979807,20.2928913882206,
7.7593675973071));
#197397=CARTESIAN_POINT('Ctrl Pts',(-20.5517980700973,20.2960403734056,
7.75958985817844));
#197398=CARTESIAN_POINT('Ctrl Pts',(-20.5481825822257,20.3020737388305,
7.76001531982343));
#197399=CARTESIAN_POINT('Ctrl Pts',(-20.5464443125057,20.3049588473293,
7.76021860518643));
#197400=CARTESIAN_POINT('Ctrl Pts',(-20.541813441999,20.3126036402632,7.7607568486212));
#197401=CARTESIAN_POINT('Ctrl Pts',(-20.5389089077131,20.3173561170672,
7.76109103068396));
#197402=CARTESIAN_POINT('Ctrl Pts',(-20.5284943718626,20.3342464888969,
7.76227741130615));
#197403=CARTESIAN_POINT('Ctrl Pts',(-20.5208802232821,20.3463201389289,
7.76312304973539));
#197404=CARTESIAN_POINT('Ctrl Pts',(-20.4262135723245,20.4931198015513,
7.77338697852945));
#197405=CARTESIAN_POINT('Ctrl Pts',(-20.3242301878234,20.6176277329912,
7.78193357094547));
#197406=CARTESIAN_POINT('Ctrl Pts',(-20.1176551141693,20.8183139245327,
7.79760618697211));
#197407=CARTESIAN_POINT('Ctrl Pts',(-20.0183307108183,20.898734786947,7.80463064801423));
#197408=CARTESIAN_POINT('Ctrl Pts',(-19.8984138110616,20.9790814700711,
7.81300661851793));
#197409=CARTESIAN_POINT('Ctrl Pts',(-19.8843372390406,20.9882720166535,
7.81398795001884));
#197410=CARTESIAN_POINT('Ctrl Pts',(-19.8618924247821,21.0025478000978,
7.81555050508725));
#197411=CARTESIAN_POINT('Ctrl Pts',(-19.8535956196823,21.0077444129569,
7.81612764833895));
#197412=CARTESIAN_POINT('Ctrl Pts',(-19.8378158724346,21.017476149014,7.81722461744339));
#197413=CARTESIAN_POINT('Ctrl Pts',(-19.8303402576475,21.0220228030466,
7.81774400818197));
#197414=CARTESIAN_POINT('Ctrl Pts',(-19.8173503255901,21.0298133493605,
7.81864610892895));
#197415=CARTESIAN_POINT('Ctrl Pts',(-19.8118490547738,21.0330788516159,
7.8190280235752));
#197416=CARTESIAN_POINT('Ctrl Pts',(-19.8011918609186,21.0393397077895,
7.81976766989241));
#197417=CARTESIAN_POINT('Ctrl Pts',(-19.7960379123843,21.0423383157185,
7.82012527859326));
#197418=CARTESIAN_POINT('Ctrl Pts',(-19.7826193281046,21.0500696581299,
7.82105612777202));
#197419=CARTESIAN_POINT('Ctrl Pts',(-19.7743353688876,21.0547684286086,
7.82163058738429));
#197420=CARTESIAN_POINT('Ctrl Pts',(-19.7460997960504,21.0705331460496,
7.8235881083859));
#197421=CARTESIAN_POINT('Ctrl Pts',(-19.7260016533377,21.0813321026709,
7.82498064918288));
#197422=CARTESIAN_POINT('Ctrl Pts',(-19.5478706013185,21.1733650465343,
7.83731985341981));
#197423=CARTESIAN_POINT('Ctrl Pts',(-19.3803952998433,21.2347121207924,
7.84899033568395));
#197424=CARTESIAN_POINT('Ctrl Pts',(-19.1239525566482,21.2935304869191,
7.86637171246791));
#197425=CARTESIAN_POINT('Ctrl Pts',(-19.0395472050749,21.307577927766,7.87200175458928));
#197426=CARTESIAN_POINT('Ctrl Pts',(-18.9172896008661,21.3203826478635,
7.87984743408718));
#197427=CARTESIAN_POINT('Ctrl Pts',(-18.8799605886957,21.3232940462605,
7.8822014619914));
#197428=CARTESIAN_POINT('Ctrl Pts',(-18.835032090921,21.3256012647865,7.88496968505304));
#197429=CARTESIAN_POINT('Ctrl Pts',(-18.8274905441352,21.3259481115464,
7.8854321492189));
#197430=CARTESIAN_POINT('Ctrl Pts',(-18.8157732354548,21.3264242100556,
7.88614709411299));
#197431=CARTESIAN_POINT('Ctrl Pts',(-18.8115987622944,21.3265814527719,
7.88640109763492));
#197432=CARTESIAN_POINT('Ctrl Pts',(-18.8038618105417,21.326849954639,7.8868705228168));
#197433=CARTESIAN_POINT('Ctrl Pts',(-18.8002995479283,21.3269645728029,
7.88708612485283));
#197434=CARTESIAN_POINT('Ctrl Pts',(-18.7922526206524,21.3272031468839,
7.88757196792881));
#197435=CARTESIAN_POINT('Ctrl Pts',(-18.7877678538963,21.3273218435374,
7.88784191181774));
#197436=CARTESIAN_POINT('Ctrl Pts',(-18.7745505751485,21.3276296185542,
7.88863512135165));
#197437=CARTESIAN_POINT('Ctrl Pts',(-18.7658171089093,21.3277789135414,
7.88915621405879));
#197438=CARTESIAN_POINT('Ctrl Pts',(-18.7033406311677,21.3284601689682,
7.89286386473415));
#197439=CARTESIAN_POINT('Ctrl Pts',(-18.6495906671543,21.3269994492115,
7.89594749674496));
#197440=CARTESIAN_POINT('Ctrl Pts',(-18.4277929341148,21.3125051277613,
7.90844343641566));
#197441=CARTESIAN_POINT('Ctrl Pts',(-18.2615422372231,21.2814777195697,
7.91731160883427));
#197442=CARTESIAN_POINT('Ctrl Pts',(-18.0440072963975,21.2132816028175,
7.92994523889008));
#197443=CARTESIAN_POINT('Ctrl Pts',(-17.9880711769933,21.1931228414789,
7.93328606720602));
#197444=CARTESIAN_POINT('Ctrl Pts',(-17.8995223143132,21.1569313091949,
7.93878049672084));
#197445=CARTESIAN_POINT('Ctrl Pts',(-17.8663436806855,21.142365824822,7.94088728903817));
#197446=CARTESIAN_POINT('Ctrl Pts',(-17.8235791965282,21.1222677714113,
7.9436731223323));
#197447=CARTESIAN_POINT('Ctrl Pts',(-17.813638829013,21.1175009418869,7.94432571525014));
#197448=CARTESIAN_POINT('Ctrl Pts',(-17.7974972358892,21.1096047017761,
7.94539386078333));
#197449=CARTESIAN_POINT('Ctrl Pts',(-17.7912733013405,21.1065219889679,
7.94580778246322));
#197450=CARTESIAN_POINT('Ctrl Pts',(-17.7793087618844,21.1005224532569,
7.94660751524662));
#197451=CARTESIAN_POINT('Ctrl Pts',(-17.7735660660613,21.097609954022,7.94699317131128));
#197452=CARTESIAN_POINT('Ctrl Pts',(-17.7604131590436,21.0908636312334,
7.94788065867894));
#197453=CARTESIAN_POINT('Ctrl Pts',(-17.7530121812613,21.0870121282368,
7.94838310969595));
#197454=CARTESIAN_POINT('Ctrl Pts',(-17.7333358995081,21.0766242289473,
7.94972724318828));
#197455=CARTESIAN_POINT('Ctrl Pts',(-17.7211020684611,21.070010535593,7.95057165702834));
#197456=CARTESIAN_POINT('Ctrl Pts',(-17.6244979286178,21.0165489989904,
7.95730995360965));
#197457=CARTESIAN_POINT('Ctrl Pts',(-17.5433670933995,20.9641088965459,
7.96340628651434));
#197458=CARTESIAN_POINT('Ctrl Pts',(-17.3555905179406,20.8236749875157,
7.97859188909507));
#197459=CARTESIAN_POINT('Ctrl Pts',(-17.2534258940791,20.7304175344374,
7.98781904442629));
#197460=CARTESIAN_POINT('Ctrl Pts',(-17.1264880300849,20.589500763277,8.00021586564108));
#197461=CARTESIAN_POINT('Ctrl Pts',(-17.0933185488935,20.549851814843,8.00355674254035));
#197462=CARTESIAN_POINT('Ctrl Pts',(-17.0449390794276,20.4875200178973,
8.00854439749442));
#197463=CARTESIAN_POINT('Ctrl Pts',(-17.0286622677056,20.465692604177,8.01024420199237));
#197464=CARTESIAN_POINT('Ctrl Pts',(-17.0088269594253,20.4379938001621,
8.01233734662302));
#197465=CARTESIAN_POINT('Ctrl Pts',(-17.0048706605102,20.432412107289,8.01275596403065));
#197466=CARTESIAN_POINT('Ctrl Pts',(-16.9986317825306,20.4235189990875,
8.01341777080889));
#197467=CARTESIAN_POINT('Ctrl Pts',(-16.9963315008191,20.420220145767,8.01366214539806));
#197468=CARTESIAN_POINT('Ctrl Pts',(-16.9919965104328,20.4139653857415,
8.01412334436727));
#197469=CARTESIAN_POINT('Ctrl Pts',(-16.9899599425139,20.4110108978688,
8.01434029081668));
#197470=CARTESIAN_POINT('Ctrl Pts',(-16.9853023300974,20.4042171087152,
8.01483710480832));
#197471=CARTESIAN_POINT('Ctrl Pts',(-16.9826864142448,20.4003743458416,
8.01511662349943));
#197472=CARTESIAN_POINT('Ctrl Pts',(-16.9757366084039,20.3900924854034,
8.01586062619177));
#197473=CARTESIAN_POINT('Ctrl Pts',(-16.9714253902685,20.3836380484482,
8.01632362143275));
#197474=CARTESIAN_POINT('Ctrl Pts',(-16.9403725292692,20.3365898217684,
8.01967033045463));
#197475=CARTESIAN_POINT('Ctrl Pts',(-16.9149983631457,20.2951059854337,
8.02246960419527));
#197476=CARTESIAN_POINT('Ctrl Pts',(-16.8776488356574,20.2290341465277,
8.02675538725693));
#197477=CARTESIAN_POINT('Ctrl Pts',(-16.8646843920881,20.205028378103,8.02827838995078));
#197478=CARTESIAN_POINT('Ctrl Pts',(-16.8320346153005,20.1416728833261,
8.03222637896995));
#197479=CARTESIAN_POINT('Ctrl Pts',(-16.8131053414653,20.1019479545533,
8.03463153073949));
#197480=CARTESIAN_POINT('Ctrl Pts',(-16.7514944818302,19.9615428790987,
8.04297926617324));
#197481=CARTESIAN_POINT('Ctrl Pts',(-16.7153842798536,19.8581726444359,
8.048866543847));
#197482=CARTESIAN_POINT('Ctrl Pts',(-16.6733296115924,19.6992227593264,
8.05800899104279));
#197483=CARTESIAN_POINT('Ctrl Pts',(-16.6613239008439,19.6454387823337,
8.06111542466533));
#197484=CARTESIAN_POINT('Ctrl Pts',(-16.6452691824588,19.557509689075,8.0662578032176));
#197485=CARTESIAN_POINT('Ctrl Pts',(-16.6399297149581,19.5236257149206,
8.0682543932694));
#197486=CARTESIAN_POINT('Ctrl Pts',(-16.6339934187422,19.4789144804222,
8.07091444373784));
#197487=CARTESIAN_POINT('Ctrl Pts',(-16.632653030641,19.468190042488,8.0715543892965));
#197488=CARTESIAN_POINT('Ctrl Pts',(-16.6305917976356,19.4506049162507,
8.07260702162063));
#197489=CARTESIAN_POINT('Ctrl Pts',(-16.6298222525402,19.4437500526939,
8.07301816753006));
#197490=CARTESIAN_POINT('Ctrl Pts',(-16.6283972524419,19.4304715502349,
8.07381622841105));
#197491=CARTESIAN_POINT('Ctrl Pts',(-16.6277376567048,19.424048425647,8.07420300810208));
#197492=CARTESIAN_POINT('Ctrl Pts',(-16.6262822125982,19.4092075189795,
8.07509842776938));
#197493=CARTESIAN_POINT('Ctrl Pts',(-16.6255073941229,19.4007878279325,
8.07560772406402));
#197494=CARTESIAN_POINT('Ctrl Pts',(-16.6235586533811,19.3781244482184,
8.07698219133443));
#197495=CARTESIAN_POINT('Ctrl Pts',(-16.6224785135233,19.3638733303569,
8.07785029143001));
#197496=CARTESIAN_POINT('Ctrl Pts',(-16.6138821960484,19.232865412346,8.08586685095066));
#197497=CARTESIAN_POINT('Ctrl Pts',(-16.6159139970288,19.1157033712371,
8.09331790069542));
#197498=CARTESIAN_POINT('Ctrl Pts',(-16.6439261312307,18.8369532615406,
8.11161841221763));
#197499=CARTESIAN_POINT('Ctrl Pts',(-16.678961738514,18.6770172015832,8.12260913299497));
#197500=CARTESIAN_POINT('Ctrl Pts',(-16.7424115425657,18.4924696231516,
8.13500301822888));
#197501=CARTESIAN_POINT('Ctrl Pts',(-16.7534868025287,18.4624826542192,
8.13700540556683));
#197502=CARTESIAN_POINT('Ctrl Pts',(-16.7678850706322,18.4260586319558,
8.13941367108017));
#197503=CARTESIAN_POINT('Ctrl Pts',(-16.7705667948012,18.4193745084273,
8.13985460542663));
#197504=CARTESIAN_POINT('Ctrl Pts',(-16.7748291971933,18.4089055001951,
8.1405434928729));
#197505=CARTESIAN_POINT('Ctrl Pts',(-16.7763868242902,18.4051113748571,
8.14079279861833));
#197506=CARTESIAN_POINT('Ctrl Pts',(-16.7793220711869,18.3980203190071,
8.14125803784942));
#197507=CARTESIAN_POINT('Ctrl Pts',(-16.7806969960787,18.3947223865673,
8.14147412369647));
#197508=CARTESIAN_POINT('Ctrl Pts',(-16.7838587973271,18.387192137581,8.14196687342175));
#197509=CARTESIAN_POINT('Ctrl Pts',(-16.7856511012649,18.3829621540919,
8.14224320387674));
#197510=CARTESIAN_POINT('Ctrl Pts',(-16.7903707548436,18.3719235536176,
8.14296319095771));
#197511=CARTESIAN_POINT('Ctrl Pts',(-16.7933201421351,18.3651243481323,
8.14340554157212));
#197512=CARTESIAN_POINT('Ctrl Pts',(-16.8130208723595,18.320353828152,8.14631173183565));
#197513=CARTESIAN_POINT('Ctrl Pts',(-16.8308512241318,18.2828638773544,
8.14871420285737));
#197514=CARTESIAN_POINT('Ctrl Pts',(-16.856854723179,18.2320945458635,8.15195670077456));
#197515=CARTESIAN_POINT('Ctrl Pts',(-16.8640879328477,18.2183474126275,
8.15283355396699));
#197516=CARTESIAN_POINT('Ctrl Pts',(-16.9510819817204,18.057336008428,8.16310429943982));
#197517=CARTESIAN_POINT('Ctrl Pts',(-17.0478976167338,17.9199526745816,
8.1719219540689));
#197518=CARTESIAN_POINT('Ctrl Pts',(-17.1991011828333,17.7518181780007,
8.18446065900252));
#197519=CARTESIAN_POINT('Ctrl Pts',(-17.240094160354,17.7098769015472,8.18775790768115));
#197520=CARTESIAN_POINT('Ctrl Pts',(-17.3088923979976,17.645099493803,8.19318708614097));
#197521=CARTESIAN_POINT('Ctrl Pts',(-17.3356318961005,17.6211753257712,
8.19527364775611));
#197522=CARTESIAN_POINT('Ctrl Pts',(-17.3713355287599,17.5908286461716,
8.19803642376453));
#197523=CARTESIAN_POINT('Ctrl Pts',(-17.3797609550363,17.5837795849484,
8.19868674200622));
#197524=CARTESIAN_POINT('Ctrl Pts',(-17.3935956969629,17.5723867368785,
8.19975209617776));
#197525=CARTESIAN_POINT('Ctrl Pts',(-17.3989722426677,17.5680033453869,
8.20016551751472));
#197526=CARTESIAN_POINT('Ctrl Pts',(-17.4093831264271,17.5596004000483,
8.20096493711652));
#197527=CARTESIAN_POINT('Ctrl Pts',(-17.4144144649471,17.5555772398776,
8.20135078385419));
#197528=CARTESIAN_POINT('Ctrl Pts',(-17.4260191713226,17.5463844029268,
8.20223964463269));
#197529=CARTESIAN_POINT('Ctrl Pts',(-17.4326049336731,17.5412306110087,
8.20274328472942));
#197530=CARTESIAN_POINT('Ctrl Pts',(-17.4502763470162,17.5275696198153,
8.20409267074068));
#197531=CARTESIAN_POINT('Ctrl Pts',(-17.4614158399239,17.5191330421731,
8.20494118178057));
#197532=CARTESIAN_POINT('Ctrl Pts',(-17.5530591320337,17.4511434569791,
8.21190585675373));
#197533=CARTESIAN_POINT('Ctrl Pts',(-17.6376005716226,17.3972691324647,
8.21824065428656));
#197534=CARTESIAN_POINT('Ctrl Pts',(-17.8766910709276,17.2677480485023,
8.23588031393972));
#197535=CARTESIAN_POINT('Ctrl Pts',(-18.0371444923131,17.2046114781734,
8.24747418828235));
#197536=CARTESIAN_POINT('Ctrl Pts',(-18.2421074788598,17.1515523289697,
8.26101541126133));
#197537=CARTESIAN_POINT('Ctrl Pts',(-18.2810361568902,17.1426414248922,
8.26353024509604));
#197538=CARTESIAN_POINT('Ctrl Pts',(-18.3277358010742,17.1333336402528,
8.26646116532803));
#197539=CARTESIAN_POINT('Ctrl Pts',(-18.3352835356523,17.1318719887964,
8.26693221048458));
#197540=CARTESIAN_POINT('Ctrl Pts',(-18.3469741293242,17.1296740578538,
8.26765751927432));
#197541=CARTESIAN_POINT('Ctrl Pts',(-18.3511114120148,17.1289089760713,
8.2679133758901));
#197542=CARTESIAN_POINT('Ctrl Pts',(-18.3587553666576,17.127518982115,8.26838452603219));
#197543=CARTESIAN_POINT('Ctrl Pts',(-18.3622613077221,17.1268905902695,
8.26860001080609));
#197544=CARTESIAN_POINT('Ctrl Pts',(-18.3701492747312,17.1254973181441,
8.2690834644603));
#197545=CARTESIAN_POINT('Ctrl Pts',(-18.3745321215583,17.1247374011151,
8.26935114908574));
#197546=CARTESIAN_POINT('Ctrl Pts',(-18.3857515363549,17.1228285354607,
8.27003405143593));
#197547=CARTESIAN_POINT('Ctrl Pts',(-18.3925914726191,17.1216993327484,
8.27044817418967));
#197548=CARTESIAN_POINT('Ctrl Pts',(-18.4325569593004,17.1153029495475,
8.27285563263566));
#197549=CARTESIAN_POINT('Ctrl Pts',(-18.4658003924063,17.1107897038376,
8.27480912193584));
#197550=CARTESIAN_POINT('Ctrl Pts',(-18.5173161577985,17.1050390230867,
8.27778010475004));
#197551=CARTESIAN_POINT('Ctrl Pts',(-18.5355192604008,17.1032455183656,
8.27881910965807));
#197552=CARTESIAN_POINT('Ctrl Pts',(-18.5848659527931,17.0990284805709,
8.28161193344054));
#197553=CARTESIAN_POINT('Ctrl Pts',(-18.6160442207572,17.0970578945792,
8.28335091143438));
#197554=CARTESIAN_POINT('Ctrl Pts',(-18.6857196928507,17.0942005329805,
8.28720145669691));
#197555=CARTESIAN_POINT('Ctrl Pts',(-18.7242204789699,17.0936725663777,
8.28930500759233));
#197556=CARTESIAN_POINT('Ctrl Pts',(-18.8719901639284,17.0956770990601,
8.29735064100863));
#197557=CARTESIAN_POINT('Ctrl Pts',(-18.980985409116,17.1056188997904,8.30323557223068));
#197558=CARTESIAN_POINT('Ctrl Pts',(-19.1429757530996,17.1331510207277,
8.31237256474343));
#197559=CARTESIAN_POINT('Ctrl Pts',(-19.1968464535868,17.1444835919757,
8.31547587219654));
#197560=CARTESIAN_POINT('Ctrl Pts',(-19.2834498064641,17.166258326963,8.32061353689087));
#197561=CARTESIAN_POINT('Ctrl Pts',(-19.3164783828135,17.1754208841652,
8.32260863380442));
#197562=CARTESIAN_POINT('Ctrl Pts',(-19.3596071713676,17.188520973581,8.32526697685399));
#197563=CARTESIAN_POINT('Ctrl Pts',(-19.3699213037584,17.1917402757332,
8.32590674664606));
#197564=CARTESIAN_POINT('Ctrl Pts',(-19.3867782964009,17.1971437319635,
8.32695916350532));
#197565=CARTESIAN_POINT('Ctrl Pts',(-19.3933360061244,17.199281182208,8.32737027095488));
#197566=CARTESIAN_POINT('Ctrl Pts',(-19.4060125448454,17.2034816725861,
8.32816830984156));
#197567=CARTESIAN_POINT('Ctrl Pts',(-19.4121326172762,17.2055407390612,
8.32855510627682));
#197568=CARTESIAN_POINT('Ctrl Pts',(-19.4262461202849,17.2103611449444,
8.32945064144796));
#197569=CARTESIAN_POINT('Ctrl Pts',(-19.4342325758616,17.2131424335383,
8.32996003703496));
#197570=CARTESIAN_POINT('Ctrl Pts',(-19.4556758288085,17.2207544329344,
8.33133494603361));
#197571=CARTESIAN_POINT('Ctrl Pts',(-19.4691005273186,17.2256736746559,
8.33220339149475));
#197572=CARTESIAN_POINT('Ctrl Pts',(-19.592328785133,17.2722496910301,8.34024729981518));
#197573=CARTESIAN_POINT('Ctrl Pts',(-19.6985198071124,17.3228329826092,
8.34772775414923));
#197574=CARTESIAN_POINT('Ctrl Pts',(-19.9414512150667,17.4644115162342,
8.366097995634));
#197575=CARTESIAN_POINT('Ctrl Pts',(-20.0728962069752,17.5630112190283,
8.37712903630611));
#197576=CARTESIAN_POINT('Ctrl Pts',(-20.2141768423464,17.697154076175,8.38949108659114));
#197577=CARTESIAN_POINT('Ctrl Pts',(-20.2362207425394,17.719026125441,8.39143502611078));
#197578=CARTESIAN_POINT('Ctrl Pts',(-20.2627314364054,17.7465136959262,
8.39378284325434));
#197579=CARTESIAN_POINT('Ctrl Pts',(-20.2676601513897,17.7516760185421,
8.39421977215372));
#197580=CARTESIAN_POINT('Ctrl Pts',(-20.2753701238397,17.7598336257244,
8.39490380395357));
#197581=CARTESIAN_POINT('Ctrl Pts',(-20.2781689225278,17.7628121517406,
8.39515222878185));
#197582=CARTESIAN_POINT('Ctrl Pts',(-20.2833998748466,17.7684114200506,
8.39561671695541));
#197583=CARTESIAN_POINT('Ctrl Pts',(-20.2858339871367,17.7710301879021,
8.39583292732478));
#197584=CARTESIAN_POINT('Ctrl Pts',(-20.2913956814051,17.7770442821801,
8.39632712641415));
#197585=CARTESIAN_POINT('Ctrl Pts',(-20.2945187948374,17.7804436742958,
8.39660477424792));
#197586=CARTESIAN_POINT('Ctrl Pts',(-20.3041550089116,17.7910014403703,
8.39746196491707));
#197587=CARTESIAN_POINT('Ctrl Pts',(-20.3106302663716,17.7981943967577,
8.39803871563367));
#197588=CARTESIAN_POINT('Ctrl Pts',(-20.3791740923844,17.8753935760489,
8.40415511606866));
#197589=CARTESIAN_POINT('Ctrl Pts',(-20.436594232468,17.9494059028784,8.40937983738445));
#197590=CARTESIAN_POINT('Ctrl Pts',(-20.5627793036262,18.1364358418443,
8.4217570558849));
#197591=CARTESIAN_POINT('Ctrl Pts',(-20.626221908922,18.2525541619432,8.42880645400543));
#197592=CARTESIAN_POINT('Ctrl Pts',(-20.7007281723604,18.4256038098187,
8.43927202716953));
#197593=CARTESIAN_POINT('Ctrl Pts',(-20.7209425133857,18.4782478969764,
8.44244777749486));
#197594=CARTESIAN_POINT('Ctrl Pts',(-20.7502231604259,18.5646645643423,
8.44769454993827));
#197595=CARTESIAN_POINT('Ctrl Pts',(-20.7605967214757,18.597965865278,8.44972408798674));
#197596=CARTESIAN_POINT('Ctrl Pts',(-20.7731190924357,18.6419652347483,
8.4524217926519));
#197597=CARTESIAN_POINT('Ctrl Pts',(-20.7760149186633,18.6524462402941,
8.45306558621039));
#197598=CARTESIAN_POINT('Ctrl Pts',(-20.780619322395,18.6696257019675,8.45412293658782));
#197599=CARTESIAN_POINT('Ctrl Pts',(-20.7823760845448,18.6763111223398,
8.45453492534631));
#197600=CARTESIAN_POINT('Ctrl Pts',(-20.785709036761,18.6892523151405,8.45533347655018));
#197601=CARTESIAN_POINT('Ctrl Pts',(-20.7872894372562,18.6955069315638,
8.45571989764198));
#197602=CARTESIAN_POINT('Ctrl Pts',(-20.7908666324012,18.7099415644316,
8.45661282583453));
#197603=CARTESIAN_POINT('Ctrl Pts',(-20.7928432517832,18.7181264252095,
8.45711997776139));
#197604=CARTESIAN_POINT('Ctrl Pts',(-20.7980153380129,18.7401173182463,
8.45848491741164));
#197605=CARTESIAN_POINT('Ctrl Pts',(-20.8011210540926,18.7539438241007,
8.45934557141486));
#197606=CARTESIAN_POINT('Ctrl Pts',(-20.835418189816,18.914138118302,8.46934714878289));
#197607=CARTESIAN_POINT('Ctrl Pts',(-20.8511375062333,19.0633573065089,
8.47899867178888));
#197608=CARTESIAN_POINT('Ctrl Pts',(-20.8508605241245,19.3627302277456,
8.49872823249889));
#197609=CARTESIAN_POINT('Ctrl Pts',(-20.8348287881732,19.5120733039284,
8.50874338999506));
#197610=CARTESIAN_POINT('Ctrl Pts',(-20.7998455026436,19.6738371168233,
8.51906813430362));
#197611=CARTESIAN_POINT('Ctrl Pts',(-20.7963536195941,19.6891562701088,
8.52004022624648));
#197612=CARTESIAN_POINT('Ctrl Pts',(-20.7913410449969,19.7100695229154,
8.5213581947173));
#197613=CARTESIAN_POINT('Ctrl Pts',(-20.7899675523737,19.7156979190889,
8.52171199357563));
#197614=CARTESIAN_POINT('Ctrl Pts',(-20.7877485339342,19.7246317738117,
8.52227205176301));
#197615=CARTESIAN_POINT('Ctrl Pts',(-20.7869181049227,19.7279409004603,
8.52247916680007));
#197616=CARTESIAN_POINT('Ctrl Pts',(-20.7851867319715,19.7347701723075,
8.52290589698809));
#197617=CARTESIAN_POINT('Ctrl Pts',(-20.784284724395,19.7382900073752,8.52312544347718));
#197618=CARTESIAN_POINT('Ctrl Pts',(-20.7821142197515,19.7466700224278,
8.52364723769655));
#197619=CARTESIAN_POINT('Ctrl Pts',(-20.7808374690448,19.7515280812075,
8.52394900964438));
#197620=CARTESIAN_POINT('Ctrl Pts',(-20.7764750779721,19.7678899464896,
8.52496307732118));
#197621=CARTESIAN_POINT('Ctrl Pts',(-20.7733095863126,19.7793724857016,
8.5256709046725));
#197622=CARTESIAN_POINT('Ctrl Pts',(-20.7559961610421,19.8401680194646,
8.52940116969203));
#197623=CARTESIAN_POINT('Ctrl Pts',(-20.7401620000124,19.8889605746082,
8.53233413666553));
#197624=CARTESIAN_POINT('Ctrl Pts',(-20.7225805753213,19.9371103879265,
8.53521114927006));
#197625=CARTESIAN_POINT('Origin',(-18.734,19.211,0.));
#197626=CARTESIAN_POINT('',(-20.7242505210392,19.9377358132316,9.55561791545399));
#197627=CARTESIAN_POINT('',(-20.7225805876262,19.9371103542273,9.33206810105871));
#197628=CARTESIAN_POINT('',(-20.7225806064498,19.9371103026755,0.));
#197629=CARTESIAN_POINT('',(-20.8516474640139,19.2128935159626,9.51094372097752));
#197630=CARTESIAN_POINT('Ctrl Pts',(-20.8516474640139,19.2128935159626,
9.51094372097752));
#197631=CARTESIAN_POINT('Ctrl Pts',(-20.8529701716602,19.3558822341493,
9.51955279572483));
#197632=CARTESIAN_POINT('Ctrl Pts',(-20.8300642449213,19.60279312627,9.53444419388365));
#197633=CARTESIAN_POINT('Ctrl Pts',(-20.7608946891188,19.8401887340949,
9.54933559204247));
#197634=CARTESIAN_POINT('Ctrl Pts',(-20.7242505210392,19.9377358132316,
9.55561791545399));
#197635=CARTESIAN_POINT('Ctrl Pts',(-20.8509991358369,19.2129128162075,
9.51057061419727));
#197636=CARTESIAN_POINT('Ctrl Pts',(-20.8511559691561,19.0393383766676,
9.5011330483765));
#197637=CARTESIAN_POINT('Ctrl Pts',(-20.8299671724295,18.8664171384252,
9.49177670366586));
#197638=CARTESIAN_POINT('Ctrl Pts',(-20.7843368967414,18.6837193760699,
9.48081374476068));
#197639=CARTESIAN_POINT('Ctrl Pts',(-20.7806161718462,18.6694573187251,
9.47995111246624));
#197640=CARTESIAN_POINT('Ctrl Pts',(-20.773518702582,18.6433701286444,9.47836008568776));
#197641=CARTESIAN_POINT('Ctrl Pts',(-20.7701872476492,18.6315332693462,
9.47763316323647));
#197642=CARTESIAN_POINT('Ctrl Pts',(-20.764734343102,18.6127866086901,9.47647366771282));
#197643=CARTESIAN_POINT('Ctrl Pts',(-20.7626802698959,18.6058573768575,
9.47604329462245));
#197644=CARTESIAN_POINT('Ctrl Pts',(-20.7587476230344,18.5928360210117,
9.4752311027985));
#197645=CARTESIAN_POINT('Ctrl Pts',(-20.7568769301004,18.5867415870071,
9.47484954600881));
#197646=CARTESIAN_POINT('Ctrl Pts',(-20.752608361724,18.5730559129435,9.4739894745682));
#197647=CARTESIAN_POINT('Ctrl Pts',(-20.7501951460048,18.5654695926931,
9.47351046013454));
#197648=CARTESIAN_POINT('Ctrl Pts',(-20.7439317413241,18.5461573762994,
9.4722852100489));
#197649=CARTESIAN_POINT('Ctrl Pts',(-20.7400217357975,18.5344513288329,
9.47153701225101));
#197650=CARTESIAN_POINT('Ctrl Pts',(-20.7162375517952,18.4652638756844,
9.4670815034937));
#197651=CARTESIAN_POINT('Ctrl Pts',(-20.6939978155362,18.4086313417106,
9.46329619240764));
#197652=CARTESIAN_POINT('Ctrl Pts',(-20.6538456531141,18.3180577755908,
9.45700994059909));
#197653=CARTESIAN_POINT('Ctrl Pts',(-20.637393387781,18.2835052489031,9.45455461815358));
#197654=CARTESIAN_POINT('Ctrl Pts',(-20.6004011271601,18.2109498055082,
9.44928102316068));
#197655=CARTESIAN_POINT('Ctrl Pts',(-20.5796160197152,18.1730911319284,
9.44645782497732));
#197656=CARTESIAN_POINT('Ctrl Pts',(-20.5313904732275,18.0912866216843,
9.44021384017038));
#197657=CARTESIAN_POINT('Ctrl Pts',(-20.5034647752896,18.0476578976974,
9.43678795584091));
#197658=CARTESIAN_POINT('Ctrl Pts',(-20.4261773035582,17.9361416352318,
9.42782578576444));
#197659=CARTESIAN_POINT('Ctrl Pts',(-20.3743265135844,17.8700829118253,
9.42230396495895));
#197660=CARTESIAN_POINT('Ctrl Pts',(-20.2941750854437,17.7795987783291,
9.41459171138658));
#197661=CARTESIAN_POINT('Ctrl Pts',(-20.2689389923727,17.752569875177,9.41226741038714));
#197662=CARTESIAN_POINT('Ctrl Pts',(-20.237711667764,17.7208331616046,9.40952769656623));
#197663=CARTESIAN_POINT('Ctrl Pts',(-20.2323883056122,17.7154805332041,
9.40906525154867));
#197664=CARTESIAN_POINT('Ctrl Pts',(-20.2240722599483,17.7072077469141,
9.40835010409874));
#197665=CARTESIAN_POINT('Ctrl Pts',(-20.2210994270836,17.7042678489612,
9.4080958804236));
#197666=CARTESIAN_POINT('Ctrl Pts',(-20.2155764514367,17.6988383289213,
9.40762625232393));
#197667=CARTESIAN_POINT('Ctrl Pts',(-20.2130287538194,17.6963463608455,
9.40741066622708));
#197668=CARTESIAN_POINT('Ctrl Pts',(-20.2072629717085,17.6907351213598,
9.40692511614676));
#197669=CARTESIAN_POINT('Ctrl Pts',(-20.2040412768835,17.6876196370761,
9.40665544774422));
#197670=CARTESIAN_POINT('Ctrl Pts',(-20.1945271404959,17.6784774433315,
9.40586379744822));
#197671=CARTESIAN_POINT('Ctrl Pts',(-20.1882072705577,17.6724792380394,
9.40534397574228));
#197672=CARTESIAN_POINT('Ctrl Pts',(-20.1430187722334,17.6301179312946,
9.40166826143151));
#197673=CARTESIAN_POINT('Ctrl Pts',(-20.1028245138211,17.5951898380279,
9.39861329471255));
#197674=CARTESIAN_POINT('Ctrl Pts',(-20.0473663573213,17.5505542303653,
9.39460933187972));
#197675=CARTESIAN_POINT('Ctrl Pts',(-20.0332369662225,17.5394753446671,
9.39360664033081));
#197676=CARTESIAN_POINT('Ctrl Pts',(-19.8680039002404,17.4132768455391,
9.38205940906762));
#197677=CARTESIAN_POINT('Ctrl Pts',(-19.7022117454792,17.3188201487658,
9.37209533211099));
#197678=CARTESIAN_POINT('Ctrl Pts',(-19.4761253839409,17.2276101249819,
9.35828423896989));
#197679=CARTESIAN_POINT('Ctrl Pts',(-19.4254688054686,17.2093867359589,
9.35518351965897));
#197680=CARTESIAN_POINT('Ctrl Pts',(-19.3621326820846,17.189293302759,9.35127493777951));
#197681=CARTESIAN_POINT('Ctrl Pts',(-19.3500557423843,17.1855805501502,
9.35052828883226));
#197682=CARTESIAN_POINT('Ctrl Pts',(-19.3309481249756,17.1798930967592,
9.34934454829694));
#197683=CARTESIAN_POINT('Ctrl Pts',(-19.3239391025258,17.1778462503868,
9.34890981937109));
#197684=CARTESIAN_POINT('Ctrl Pts',(-19.3107990751556,17.1740826324432,
9.34809380708692));
#197685=CARTESIAN_POINT('Ctrl Pts',(-19.3046706277604,17.1723571748354,
9.3477128120859));
#197686=CARTESIAN_POINT('Ctrl Pts',(-19.2909642967012,17.1685648191219,
9.34685975621558));
#197687=CARTESIAN_POINT('Ctrl Pts',(-19.2833825342924,17.1665124054402,
9.34638723044095));
#197688=CARTESIAN_POINT('Ctrl Pts',(-19.2641915353184,17.1614317823313,
9.34518944998548));
#197689=CARTESIAN_POINT('Ctrl Pts',(-19.2525677664978,17.15846001129,9.3444623809298));
#197690=CARTESIAN_POINT('Ctrl Pts',(-19.1869849573172,17.1422855431112,
9.34035074575119));
#197691=CARTESIAN_POINT('Ctrl Pts',(-19.1325521135701,17.1311129391091,
9.33690150386763));
#197692=CARTESIAN_POINT('Ctrl Pts',(-19.0530877062572,17.1180364154442,
9.33181011684537));
#197693=CARTESIAN_POINT('Ctrl Pts',(-19.0283595798706,17.1144156598576,
9.3302181370853));
#197694=CARTESIAN_POINT('Ctrl Pts',(-18.8435190769908,17.0906853214812,
9.31826531538477));
#197695=CARTESIAN_POINT('Ctrl Pts',(-18.6816452567446,17.0885064889055,
9.30744571711568));
#197696=CARTESIAN_POINT('Ctrl Pts',(-18.472364140057,17.1096582020175,9.29371900255726));
#197697=CARTESIAN_POINT('Ctrl Pts',(-18.4237880965037,17.1162780889317,
9.29055634194354));
#197698=CARTESIAN_POINT('Ctrl Pts',(-18.3495961162417,17.1290267639684,
9.28580257402245));
#197699=CARTESIAN_POINT('Ctrl Pts',(-18.323793152767,17.1339565746499,9.28416376714254));
#197700=CARTESIAN_POINT('Ctrl Pts',(-18.2914718063994,17.1407576227936,
9.28213485044928));
#197701=CARTESIAN_POINT('Ctrl Pts',(-18.2848629142585,17.1421813555613,
9.28172125283126));
#197702=CARTESIAN_POINT('Ctrl Pts',(-18.2743511524818,17.1444986170921,
9.28106554524337));
#197703=CARTESIAN_POINT('Ctrl Pts',(-18.2704438668137,17.1453715870018,
9.28082228646957));
#197704=CARTESIAN_POINT('Ctrl Pts',(-18.2630347853453,17.1470490132159,
9.28036194045529));
#197705=CARTESIAN_POINT('Ctrl Pts',(-18.2595326054409,17.147851289675,9.28014473815641));
#197706=CARTESIAN_POINT('Ctrl Pts',(-18.2514718861814,17.1497194429433,
9.2796457108216));
#197707=CARTESIAN_POINT('Ctrl Pts',(-18.2469148297085,17.150791526721,9.27936424543075));
#197708=CARTESIAN_POINT('Ctrl Pts',(-18.2347025832605,17.1537073398141,
9.27861162665503));
#197709=CARTESIAN_POINT('Ctrl Pts',(-18.2270539768432,17.1555786967189,
9.27814201695103));
#197710=CARTESIAN_POINT('Ctrl Pts',(-18.1696396492156,17.1699660343753,
9.2746289165798));
#197711=CARTESIAN_POINT('Ctrl Pts',(-18.1203289767207,17.1842461798905,
9.2716796097489));
#197712=CARTESIAN_POINT('Ctrl Pts',(-18.0580841587589,17.2047525718405,
9.26798767910132));
#197713=CARTESIAN_POINT('Ctrl Pts',(-18.0446311652383,17.2093352952193,
9.26719163207716));
#197714=CARTESIAN_POINT('Ctrl Pts',(-17.8962977516328,17.2615374856272,
9.25842527575048));
#197715=CARTESIAN_POINT('Ctrl Pts',(-17.7665260879398,17.3225754600111,
9.25083107093263));
#197716=CARTESIAN_POINT('Ctrl Pts',(-17.5641927797872,17.4441143205237,
9.23783246533079));
#197717=CARTESIAN_POINT('Ctrl Pts',(-17.4877379719492,17.497184957882,9.23261225904014));
#197718=CARTESIAN_POINT('Ctrl Pts',(-17.3985182025594,17.5682514972969,
9.22596832926444));
#197719=CARTESIAN_POINT('Ctrl Pts',(-17.3822107581231,17.5816442768511,
9.22472990058551));
#197720=CARTESIAN_POINT('Ctrl Pts',(-17.3592678173514,17.6010681013727,
9.2229515322736));
#197721=CARTESIAN_POINT('Ctrl Pts',(-17.3524658875809,17.6069012546947,
9.22241968175527));
#197722=CARTESIAN_POINT('Ctrl Pts',(-17.3407808917075,17.6170514455098,
9.22149790146752));
#197723=CARTESIAN_POINT('Ctrl Pts',(-17.3358803166845,17.6213482055074,
9.22110881587689));
#197724=CARTESIAN_POINT('Ctrl Pts',(-17.3265251231498,17.6296274398158,
9.22036120163581));
#197725=CARTESIAN_POINT('Ctrl Pts',(-17.3220673647039,17.6336062839874,
9.22000282723378));
#197726=CARTESIAN_POINT('Ctrl Pts',(-17.3104975240537,17.6440214714459,
9.21906706637876));
#197727=CARTESIAN_POINT('Ctrl Pts',(-17.3034122950557,17.6504873208781,
9.21848843516319));
#197728=CARTESIAN_POINT('Ctrl Pts',(-17.2792900875575,17.672803150644,9.21649902038868));
#197729=CARTESIAN_POINT('Ctrl Pts',(-17.2624710974058,17.6888853204343,
9.21507832483139));
#197730=CARTESIAN_POINT('Ctrl Pts',(-17.1239831722456,17.8257471635445,
9.20309061536465));
#197731=CARTESIAN_POINT('Ctrl Pts',(-17.0171565492406,17.9605975606064,
9.19185603875112));
#197732=CARTESIAN_POINT('Ctrl Pts',(-16.8808909923973,18.1835007217766,
9.17459208411309));
#197733=CARTESIAN_POINT('Ctrl Pts',(-16.8389388339357,18.2631007839323,
9.16866114095377));
#197734=CARTESIAN_POINT('Ctrl Pts',(-16.7864087608085,18.3802998744849,
9.16045626214705));
#197735=CARTESIAN_POINT('Ctrl Pts',(-16.7716077329849,18.4158953805543,
9.15803083968417));
#197736=CARTESIAN_POINT('Ctrl Pts',(-16.7550562675883,18.458983610703,9.15519024499545));
#197737=CARTESIAN_POINT('Ctrl Pts',(-16.7523649478733,18.4661043898327,
9.15472388324137));
#197738=CARTESIAN_POINT('Ctrl Pts',(-16.7482515035196,18.4771679528309,
9.1540042293374));
#197739=CARTESIAN_POINT('Ctrl Pts',(-16.7468026116876,18.4811006197332,
9.15374938268126));
#197740=CARTESIAN_POINT('Ctrl Pts',(-16.7441435620844,18.4883845755958,
9.15327917737922));
#197741=CARTESIAN_POINT('Ctrl Pts',(-16.7429301961312,18.4917345889518,
9.15306363339954));
#197742=CARTESIAN_POINT('Ctrl Pts',(-16.7402140829829,18.4992931178714,
9.15257889885626));
#197743=CARTESIAN_POINT('Ctrl Pts',(-16.7387162044095,18.5035033251944,
9.15230999948717));
#197744=CARTESIAN_POINT('Ctrl Pts',(-16.7343571326063,18.5158796694874,
9.15152269448925));
#197745=CARTESIAN_POINT('Ctrl Pts',(-16.7315326211589,18.5240587554339,
9.15100641371015));
#197746=CARTESIAN_POINT('Ctrl Pts',(-16.712151895311,18.5813159653651,9.14741874754831));
#197747=CARTESIAN_POINT('Ctrl Pts',(-16.6973501207357,18.6309741794751,
9.14444287593275));
#197748=CARTESIAN_POINT('Ctrl Pts',(-16.679004293762,18.7019385099139,9.14031538506015));
#197749=CARTESIAN_POINT('Ctrl Pts',(-16.6739418011842,18.7228287039686,
9.13911544917261));
#197750=CARTESIAN_POINT('Ctrl Pts',(-16.6387809784156,18.8782204368672,
9.13027795592624));
#197751=CARTESIAN_POINT('Ctrl Pts',(-16.6215632619407,19.0152994916703,
9.12294767849478));
#197752=CARTESIAN_POINT('Ctrl Pts',(-16.6153091871384,19.2438168920291,
9.11034425721557));
#197753=CARTESIAN_POINT('Ctrl Pts',(-16.6186639937089,19.3346064462657,
9.10524191930659));
#197754=CARTESIAN_POINT('Ctrl Pts',(-16.6299381193021,19.4456200996201,
9.09874059515106));
#197755=CARTESIAN_POINT('Ctrl Pts',(-16.6323487084567,19.4663131254915,
9.09751773049638));
#197756=CARTESIAN_POINT('Ctrl Pts',(-16.6362262961191,19.4958051188765,
9.0957578566073));
#197757=CARTESIAN_POINT('Ctrl Pts',(-16.6374441697689,19.5046360254691,
9.09522870481878));
#197758=CARTESIAN_POINT('Ctrl Pts',(-16.6396477609538,19.5199013915578,
9.09431011127916));
#197759=CARTESIAN_POINT('Ctrl Pts',(-16.6406074540549,19.5263395281692,
9.09392149780407));
#197760=CARTESIAN_POINT('Ctrl Pts',(-16.6425065464657,19.538688811675,9.09317373918762));
#197761=CARTESIAN_POINT('Ctrl Pts',(-16.643441353199,19.5446006094361,9.09281474324452));
#197762=CARTESIAN_POINT('Ctrl Pts',(-16.6459483385153,19.5600305509882,
9.09187501990433));
#197763=CARTESIAN_POINT('Ctrl Pts',(-16.6475605171581,19.5695419726771,
9.0912930269693));
#197764=CARTESIAN_POINT('Ctrl Pts',(-16.6533405544899,19.6022828199195,
9.08928007747117));
#197765=CARTESIAN_POINT('Ctrl Pts',(-16.6578316888106,19.6254527068738,
9.08783889123328));
#197766=CARTESIAN_POINT('Ctrl Pts',(-16.6968550896355,19.8101865676598,
9.07621033483751));
#197767=CARTESIAN_POINT('Ctrl Pts',(-16.7497996744501,19.9672494842331,
9.06540847775969));
#197768=CARTESIAN_POINT('Ctrl Pts',(-16.8749459872598,20.2317073680745,
9.04607396881135));
#197769=CARTESIAN_POINT('Ctrl Pts',(-16.9397429627165,20.341740366408,9.0376463430569));
#197770=CARTESIAN_POINT('Ctrl Pts',(-17.0210404075602,20.4550266046997,
9.02899835365822));
#197771=CARTESIAN_POINT('Ctrl Pts',(-17.0281137779997,20.4647084874021,
9.02825964815667));
#197772=CARTESIAN_POINT('Ctrl Pts',(-17.0382747683764,20.4783714156561,
9.02721836220784));
#197773=CARTESIAN_POINT('Ctrl Pts',(-17.0412947758136,20.4824021360694,
9.02691131657579));
#197774=CARTESIAN_POINT('Ctrl Pts',(-17.0465196730008,20.4893240456284,
9.02638433797518));
#197775=CARTESIAN_POINT('Ctrl Pts',(-17.0487176698331,20.4922203901149,
9.02616392744933));
#197776=CARTESIAN_POINT('Ctrl Pts',(-17.0529903498914,20.4978205666287,
9.02573795867371));
#197777=CARTESIAN_POINT('Ctrl Pts',(-17.055064100227,20.5005250518273,9.02553233522139));
#197778=CARTESIAN_POINT('Ctrl Pts',(-17.0606692116394,20.5077985265467,
9.02497953393736));
#197779=CARTESIAN_POINT('Ctrl Pts',(-17.0642127810733,20.5123581332659,
9.02463321175031));
#197780=CARTESIAN_POINT('Ctrl Pts',(-17.0773898817796,20.5291710285477,
9.02335677304543));
#197781=CARTESIAN_POINT('Ctrl Pts',(-17.0871402614938,20.5413326568561,
9.02243459462963));
#197782=CARTESIAN_POINT('Ctrl Pts',(-17.1836996709749,20.6590822551381,
9.01350490219508));
#197783=CARTESIAN_POINT('Ctrl Pts',(-17.2804207792035,20.7561508504849,
9.00612147989973));
#197784=CARTESIAN_POINT('Ctrl Pts',(-17.5049797301052,20.9416288576053,
8.99030488527974));
#197785=CARTESIAN_POINT('Ctrl Pts',(-17.6345190125573,21.0266820112385,
8.98188548047938));
#197786=CARTESIAN_POINT('Ctrl Pts',(-17.791100556187,21.10654268022,8.9716490606345));
#197787=CARTESIAN_POINT('Ctrl Pts',(-17.8101924758871,21.1159202144791,
8.97040088994565));
#197788=CARTESIAN_POINT('Ctrl Pts',(-17.8375492478874,21.1288492786132,
8.96861095540869));
#197789=CARTESIAN_POINT('Ctrl Pts',(-17.8457008261013,21.1326384624313,
8.96807742739034));
#197790=CARTESIAN_POINT('Ctrl Pts',(-17.8598084692161,21.1390873198482,
8.96715366293316));
#197791=CARTESIAN_POINT('Ctrl Pts',(-17.8657531920121,21.1417716137348,
8.96676428058841));
#197792=CARTESIAN_POINT('Ctrl Pts',(-17.8771616963411,21.1468596932149,
8.96601674208702));
#197793=CARTESIAN_POINT('Ctrl Pts',(-17.8826234330424,21.1492679305329,
8.96565874328606));
#197794=CARTESIAN_POINT('Ctrl Pts',(-17.8968576550487,21.1554724380157,
8.96472538742464));
#197795=CARTESIAN_POINT('Ctrl Pts',(-17.9056457241828,21.1592324186198,
8.96414879816729));
#197796=CARTESIAN_POINT('Ctrl Pts',(-17.935727412096,21.1718625575481,8.96217377747856));
#197797=CARTESIAN_POINT('Ctrl Pts',(-17.9571398155571,21.1804439017053,
8.96076562643059));
#197798=CARTESIAN_POINT('Ctrl Pts',(-18.1416935738649,21.2509286223824,
8.94860483103081));
#197799=CARTESIAN_POINT('Ctrl Pts',(-18.3117420805782,21.2927806997673,
8.9371575300774));
#197800=CARTESIAN_POINT('Ctrl Pts',(-18.5720579469652,21.3236185719297,
8.91983713730217));
#197801=CARTESIAN_POINT('Ctrl Pts',(-18.6597239996754,21.3285144555854,
8.91405464175905));
#197802=CARTESIAN_POINT('Ctrl Pts',(-18.785444532426,21.3277159552842,8.90602656685559));
#197803=CARTESIAN_POINT('Ctrl Pts',(-18.8234328776712,21.3264515241592,
8.90363600516227));
#197804=CARTESIAN_POINT('Ctrl Pts',(-18.8689372378835,21.323708788634,8.90083072035237));
#197805=CARTESIAN_POINT('Ctrl Pts',(-18.8765029332506,21.3232119689433,
8.90036624367531));
#197806=CARTESIAN_POINT('Ctrl Pts',(-18.8882398338724,21.3223778873363,
8.89964886696501));
#197807=CARTESIAN_POINT('Ctrl Pts',(-18.8924128945056,21.3220688915901,
8.89939442779831));
#197808=CARTESIAN_POINT('Ctrl Pts',(-18.9001380735038,21.3214738423841,
8.89892460053718));
#197809=CARTESIAN_POINT('Ctrl Pts',(-18.9036903552748,21.3211911957173,
8.89870902950286));
#197810=CARTESIAN_POINT('Ctrl Pts',(-18.9117040921103,21.3205331948636,
8.89822376376608));
#197811=CARTESIAN_POINT('Ctrl Pts',(-18.9161650673336,21.3201526577454,
8.89795436311789));
#197812=CARTESIAN_POINT('Ctrl Pts',(-18.9292829712937,21.318991724684,8.89716422695986));
#197813=CARTESIAN_POINT('Ctrl Pts',(-18.9379364606908,21.3181721515048,
8.89664563929106));
#197814=CARTESIAN_POINT('Ctrl Pts',(-18.9990565093854,21.3120034199951,
8.89299996408863));
#197815=CARTESIAN_POINT('Ctrl Pts',(-19.0513167611672,21.3047481667129,
8.88997194202517));
#197816=CARTESIAN_POINT('Ctrl Pts',(-19.1187993044587,21.2927943406484,
8.88611580630671));
#197817=CARTESIAN_POINT('Ctrl Pts',(-19.1343118021733,21.2898671578818,
8.88523312987995));
#197818=CARTESIAN_POINT('Ctrl Pts',(-19.199642153134,21.2767810383419,8.8815263668416));
#197819=CARTESIAN_POINT('Ctrl Pts',(-19.2491197703036,21.265002405892,8.87874487264263));
#197820=CARTESIAN_POINT('Ctrl Pts',(-19.4035795705845,21.2222987070093,
8.87001965697419));
#197821=CARTESIAN_POINT('Ctrl Pts',(-19.5066125666359,21.1850132307558,
8.86412867689407));
#197822=CARTESIAN_POINT('Ctrl Pts',(-19.656577444329,21.1171964308693,8.85497762160709));
#197823=CARTESIAN_POINT('Ctrl Pts',(-19.7059453446942,21.0925035405958,
8.85186625349982));
#197824=CARTESIAN_POINT('Ctrl Pts',(-19.78437845965,21.0493615848196,8.84671643539947));
#197825=CARTESIAN_POINT('Ctrl Pts',(-19.814058467919,21.0320825719288,8.8447174897858));
#197826=CARTESIAN_POINT('Ctrl Pts',(-19.8525132503375,21.0084242741805,
8.84205474589328));
#197827=CARTESIAN_POINT('Ctrl Pts',(-19.8616788879715,21.0026880955267,
8.84141452329861));
#197828=CARTESIAN_POINT('Ctrl Pts',(-19.8766199767308,20.9931773718663,
8.84036155136416));
#197829=CARTESIAN_POINT('Ctrl Pts',(-19.8824217014148,20.9894443173751,
8.83995034483313));
#197830=CARTESIAN_POINT('Ctrl Pts',(-19.8936175176188,20.9821628663962,
8.8391522492247));
#197831=CARTESIAN_POINT('Ctrl Pts',(-19.8990138330768,20.9786180169302,
8.83876549586705));
#197832=CARTESIAN_POINT('Ctrl Pts',(-19.9114372720954,20.9703754343297,
8.83787025796834));
#197833=CARTESIAN_POINT('Ctrl Pts',(-19.9184526093742,20.965660212563,8.8373611179472));
#197834=CARTESIAN_POINT('Ctrl Pts',(-19.9372457763804,20.952864692812,8.83598734578536));
#197835=CARTESIAN_POINT('Ctrl Pts',(-19.9489702229855,20.9447071113675,
8.83511978913189));
#197836=CARTESIAN_POINT('Ctrl Pts',(-20.0755780769391,20.8547014682906,
8.82563481138858));
#197837=CARTESIAN_POINT('Ctrl Pts',(-20.1820673788121,20.7617010578141,
8.81656769436383));
#197838=CARTESIAN_POINT('Ctrl Pts',(-20.3445945741313,20.5883208222221,
8.80093331629477));
#197839=CARTESIAN_POINT('Ctrl Pts',(-20.4057792424103,20.5133754808729,
8.7945051455001));
#197840=CARTESIAN_POINT('Ctrl Pts',(-20.4993339082288,20.3812739366933,
8.78394200650054));
#197841=CARTESIAN_POINT('Ctrl Pts',(-20.5345602895933,20.3263157282221,
8.77974788110164));
#197842=CARTESIAN_POINT('Ctrl Pts',(-20.5737749596308,20.2584207312087,
8.77487643836234));
#197843=CARTESIAN_POINT('Ctrl Pts',(-20.5802489430024,20.2469666745198,
8.77406484960454));
#197844=CARTESIAN_POINT('Ctrl Pts',(-20.5891459478426,20.2308773685124,
8.77293985106746));
#197845=CARTESIAN_POINT('Ctrl Pts',(-20.5916590613372,20.2262926414462,
8.7726209663652));
#197846=CARTESIAN_POINT('Ctrl Pts',(-20.5959079048546,20.2184727944828,
8.77207999840212));
#197847=CARTESIAN_POINT('Ctrl Pts',(-20.5976522424459,20.2152423998883,
8.77185737102709));
#197848=CARTESIAN_POINT('Ctrl Pts',(-20.6009776731038,20.2090454238673,
8.77143194155917));
#197849=CARTESIAN_POINT('Ctrl Pts',(-20.6025601088368,20.2060796048557,
8.77122905136491));
#197850=CARTESIAN_POINT('Ctrl Pts',(-20.6067291659063,20.198220898131,8.77069330195796));
#197851=CARTESIAN_POINT('Ctrl Pts',(-20.6093036962946,20.1933215760522,
8.77036120535277));
#197852=CARTESIAN_POINT('Ctrl Pts',(-20.6183487943044,20.175943626707,8.76918977970356));
#197853=CARTESIAN_POINT('Ctrl Pts',(-20.6247144238561,20.1634104012543,
8.76835679554186));
#197854=CARTESIAN_POINT('Ctrl Pts',(-20.6654151976915,20.0812585002503,
8.76296778464621));
#197855=CARTESIAN_POINT('Ctrl Pts',(-20.6959972507266,20.0099135291362,
8.75861679153289));
#197856=CARTESIAN_POINT('Ctrl Pts',(-20.7225807266241,19.9371099735572,
8.75434675637709));
#197857=CARTESIAN_POINT('',(-20.8509999019989,19.2103558441126,9.29097300469246));
#197858=CARTESIAN_POINT('Ctrl Pts',(-20.7225805753213,19.9371103879265,
8.53521114927006));
#197859=CARTESIAN_POINT('Ctrl Pts',(-20.697266443062,20.0064375763663,8.5393535369811));
#197860=CARTESIAN_POINT('Ctrl Pts',(-20.6683301049202,20.0744322566373,
8.54338088181996));
#197861=CARTESIAN_POINT('Ctrl Pts',(-20.5622080177643,20.2914993392095,
8.55651379520119));
#197862=CARTESIAN_POINT('Ctrl Pts',(-20.4709008767018,20.432880427387,8.56556724285402));
#197863=CARTESIAN_POINT('Ctrl Pts',(-20.3488895873905,20.580076994319,8.57667163327324));
#197864=CARTESIAN_POINT('Ctrl Pts',(-20.3336077786475,20.5979012529915,
8.57804663419689));
#197865=CARTESIAN_POINT('Ctrl Pts',(-20.3116466052538,20.6226702379959,
8.58000263285212));
#197866=CARTESIAN_POINT('Ctrl Pts',(-20.3052111021477,20.6298295668434,
8.5805734762658));
#197867=CARTESIAN_POINT('Ctrl Pts',(-20.2946981104799,20.6413657526999,
8.58150235508359));
#197868=CARTESIAN_POINT('Ctrl Pts',(-20.2906504611549,20.6457697094684,
8.58185912434024));
#197869=CARTESIAN_POINT('Ctrl Pts',(-20.2821571010096,20.6549324779371,
8.58260599037739));
#197870=CARTESIAN_POINT('Ctrl Pts',(-20.2777079926067,20.6596880417603,
8.58299623058215));
#197871=CARTESIAN_POINT('Ctrl Pts',(-20.2671051411325,20.6709169147557,
8.58392392879231));
#197872=CARTESIAN_POINT('Ctrl Pts',(-20.2609322715509,20.6773719194094,
8.58446221059677));
#197873=CARTESIAN_POINT('Ctrl Pts',(-20.2401569293829,20.6988233858868,
8.58626796294337));
#197874=CARTESIAN_POINT('Ctrl Pts',(-20.2253732824973,20.7136419421783,
8.58754334280867));
#197875=CARTESIAN_POINT('Ctrl Pts',(-20.1447384681493,20.7921049169803,
8.5944510628809));
#197876=CARTESIAN_POINT('Ctrl Pts',(-20.0750377662661,20.8516369818007,
8.60025771159307));
#197877=CARTESIAN_POINT('Ctrl Pts',(-19.926079662512,20.9630139522418,8.61232145198565));
#197878=CARTESIAN_POINT('Ctrl Pts',(-19.8467534181857,21.0144369746358,
8.61857374253698));
#197879=CARTESIAN_POINT('Ctrl Pts',(-19.6994150782486,21.0965167257679,
8.62971096555022));
#197880=CARTESIAN_POINT('Ctrl Pts',(-19.6327063832409,21.1292094997095,
8.6345931002256));
#197881=CARTESIAN_POINT('Ctrl Pts',(-19.525553203944,21.1749036061143,8.64206180819788));
#197882=CARTESIAN_POINT('Ctrl Pts',(-19.4862011987982,21.1903099195942,
8.64472892160001));
#197883=CARTESIAN_POINT('Ctrl Pts',(-19.4393956551154,21.2070364423741,
8.64779180719334));
#197884=CARTESIAN_POINT('Ctrl Pts',(-19.4323664138277,21.2095066588165,
8.64824892665264));
#197885=CARTESIAN_POINT('Ctrl Pts',(-19.420970858578,21.2134438201632,8.64898519812854));
#197886=CARTESIAN_POINT('Ctrl Pts',(-19.416612612505,21.2149336904248,8.64926565607755));
#197887=CARTESIAN_POINT('Ctrl Pts',(-19.4088636481995,21.2175544676354,
8.64976226145896));
#197888=CARTESIAN_POINT('Ctrl Pts',(-19.405474898281,21.2186910212727,8.64997873911183));
#197889=CARTESIAN_POINT('Ctrl Pts',(-19.3981986884573,21.2211109075731,
8.65044205126195));
#197890=CARTESIAN_POINT('Ctrl Pts',(-19.3943103909334,21.2223915448691,
8.65068872632256));
#197891=CARTESIAN_POINT('Ctrl Pts',(-19.383604480465,21.2258832191108,8.6513654696876));
#197892=CARTESIAN_POINT('Ctrl Pts',(-19.3767792431543,21.2280709495722,
8.65179418719733));
#197893=CARTESIAN_POINT('Ctrl Pts',(-19.3399295084886,21.2396765602429,
8.6540948708341));
#197894=CARTESIAN_POINT('Ctrl Pts',(-19.3097072531193,21.2484593376342,
8.6559318753607));
#197895=CARTESIAN_POINT('Ctrl Pts',(-19.1212225145105,21.2987048423835,
8.66714524680859));
#197896=CARTESIAN_POINT('Ctrl Pts',(-18.9587779355933,21.3223834116316,
8.67579058385937));
#197897=CARTESIAN_POINT('Ctrl Pts',(-18.6781394172706,21.3305013979011,
8.6911590786924));
#197898=CARTESIAN_POINT('Ctrl Pts',(-18.5610028501522,21.3241666469738,
8.69769654112037));
#197899=CARTESIAN_POINT('Ctrl Pts',(-18.4308397135022,21.3062296178131,
8.70539395836518));
#197900=CARTESIAN_POINT('Ctrl Pts',(-18.4167001939912,21.3041350001508,
8.7062356886414));
#197901=CARTESIAN_POINT('Ctrl Pts',(-18.3942316654552,21.3005736358623,
8.70758255783291));
#197902=CARTESIAN_POINT('Ctrl Pts',(-18.3858882084579,21.2991998655002,
8.70808475354811));
#197903=CARTESIAN_POINT('Ctrl Pts',(-18.3711884695228,21.2966889716256,
8.70897324183996));
#197904=CARTESIAN_POINT('Ctrl Pts',(-18.364828704794,21.2955726771639,8.70935886802469));
#197905=CARTESIAN_POINT('Ctrl Pts',(-18.3516858572312,21.2932037544248,
8.71015836788225));
#197906=CARTESIAN_POINT('Ctrl Pts',(-18.3449035980984,21.2919470360817,
8.71057236772773));
#197907=CARTESIAN_POINT('Ctrl Pts',(-18.3275113943058,21.2886363499116,
8.71163773059789));
#197908=CARTESIAN_POINT('Ctrl Pts',(-18.3169109127072,21.2865342626689,
8.71229062230758));
#197909=CARTESIAN_POINT('Ctrl Pts',(-18.2727439655658,21.2774238885508,
8.71502605984439));
#197910=CARTESIAN_POINT('Ctrl Pts',(-18.2393357130508,21.2696820647382,
8.71713192371956));
#197911=CARTESIAN_POINT('Ctrl Pts',(-18.1527992335397,21.247400644919,8.72268620213861));
#197912=CARTESIAN_POINT('Ctrl Pts',(-18.1000269286452,21.2315937847153,
8.72617299869131));
#197913=CARTESIAN_POINT('Ctrl Pts',(-17.944468683369,21.1783054266116,8.73674197945718));
#197914=CARTESIAN_POINT('Ctrl Pts',(-17.843912389027,21.1348999245577,8.74397255635639));
#197915=CARTESIAN_POINT('Ctrl Pts',(-17.7067680854319,21.0626395000149,
8.75421258502946));
#197916=CARTESIAN_POINT('Ctrl Pts',(-17.6670667403258,21.040051080264,8.75722349561681));
#197917=CARTESIAN_POINT('Ctrl Pts',(-17.6086446024923,21.0042613295778,
8.7616987443569));
#197918=CARTESIAN_POINT('Ctrl Pts',(-17.5893569571793,20.9920118820241,
8.76318373530252));
#197919=CARTESIAN_POINT('Ctrl Pts',(-17.5696866576269,20.9790678521909,
8.76470338976718));
#197920=CARTESIAN_POINT('Ctrl Pts',(-17.5691025874667,20.9786830902211,
8.76474851762825));
#197921=CARTESIAN_POINT('Ctrl Pts',(-17.5591782945465,20.9721383097217,
8.76551539240275));
#197922=CARTESIAN_POINT('Ctrl Pts',(-17.5498867106956,20.9659045306252,
8.76623457765257));
#197923=CARTESIAN_POINT('Ctrl Pts',(-17.507398438208,20.9369078029994,8.76952734238311));
#197924=CARTESIAN_POINT('Ctrl Pts',(-17.4748033299085,20.9132729997179,
8.77206510497319));
#197925=CARTESIAN_POINT('Ctrl Pts',(-17.4370801352088,20.8842428960584,
8.77499764394009));
#197926=CARTESIAN_POINT('Ctrl Pts',(-17.4312837722089,20.8797340586053,
8.77544811122722));
#197927=CARTESIAN_POINT('Ctrl Pts',(-17.4219156215332,20.872368261596,8.77617578407163));
#197928=CARTESIAN_POINT('Ctrl Pts',(-17.4183294818204,20.8695297722246,
8.77645424746876));
#197929=CARTESIAN_POINT('Ctrl Pts',(-17.4119596097382,20.864454250754,8.77694866223357));
#197930=CARTESIAN_POINT('Ctrl Pts',(-17.4091723176459,20.8622217796344,
8.77716493276392));
#197931=CARTESIAN_POINT('Ctrl Pts',(-17.4031854246193,20.8574016819738,
8.77762930085621));
#197932=CARTESIAN_POINT('Ctrl Pts',(-17.3999877246197,20.8548117843139,
8.77787723108875));
#197933=CARTESIAN_POINT('Ctrl Pts',(-17.3911665577945,20.8476246069269,
8.77856096723779));
#197934=CARTESIAN_POINT('Ctrl Pts',(-17.3855591068744,20.8430076343961,
8.77899537564996));
#197935=CARTESIAN_POINT('Ctrl Pts',(-17.3547167627444,20.8173456758358,
8.7813841566111));
#197936=CARTESIAN_POINT('Ctrl Pts',(-17.3299492133875,20.7957429876211,
8.78330032437692));
#197937=CARTESIAN_POINT('Ctrl Pts',(-17.1858166763207,20.6639950709991,
8.79450824017));
#197938=CARTESIAN_POINT('Ctrl Pts',(-17.0789354462819,20.5409771900929,
8.80309316148495));
#197939=CARTESIAN_POINT('Ctrl Pts',(-16.9212132977192,20.3106014038456,
8.81837806893171));
#197940=CARTESIAN_POINT('Ctrl Pts',(-16.8633508000439,20.2089905778889,
8.82489580739017));
#197941=CARTESIAN_POINT('Ctrl Pts',(-16.8081397131977,20.0901787794864,
8.83257102198007));
#197942=CARTESIAN_POINT('Ctrl Pts',(-16.8022496382064,20.0771603173696,
8.83341246760097));
#197943=CARTESIAN_POINT('Ctrl Pts',(-16.7930850546525,20.0563458769969,
8.83475896639015));
#197944=CARTESIAN_POINT('Ctrl Pts',(-16.7897246222875,20.0485880427077,
8.83526107892037));
#197945=CARTESIAN_POINT('Ctrl Pts',(-16.7838798922056,20.0348702902614,
8.83614947031357));
#197946=CARTESIAN_POINT('Ctrl Pts',(-16.7813762090455,20.0289187120811,
8.83653508325107));
#197947=CARTESIAN_POINT('Ctrl Pts',(-16.7762540305768,20.0165850705351,
8.83733460501504));
#197948=CARTESIAN_POINT('Ctrl Pts',(-16.7736394274112,20.0102014829498,
8.83774864025748));
#197949=CARTESIAN_POINT('Ctrl Pts',(-16.7670079847104,19.9937823820435,
8.83881419820976));
#197950=CARTESIAN_POINT('Ctrl Pts',(-16.7630367604073,19.9837287669281,
8.83946725068541));
#197951=CARTESIAN_POINT('Ctrl Pts',(-16.7467815462405,19.941636163221,8.84220424622047));
#197952=CARTESIAN_POINT('Ctrl Pts',(-16.735200988927,19.9093327880421,8.84431154056221));
#197953=CARTESIAN_POINT('Ctrl Pts',(-16.7070758831044,19.8244379469762,
8.84987049159078));
#197954=CARTESIAN_POINT('Ctrl Pts',(-16.6917922885381,19.7714590369049,
8.85336061084803));
#197955=CARTESIAN_POINT('Ctrl Pts',(-16.6523943002885,19.6117209069783,
8.86393597418552));
#197956=CARTESIAN_POINT('Ctrl Pts',(-16.6344706181297,19.5036302164386,
8.8711695896824));
#197957=CARTESIAN_POINT('Ctrl Pts',(-16.6206897590714,19.3453708529905,
8.88166329541942));
#197958=CARTESIAN_POINT('Ctrl Pts',(-16.6181270523272,19.2959566120396,
8.88492412782601));
#197959=CARTESIAN_POINT('Ctrl Pts',(-16.6170179167089,19.2298180558959,
8.88923735167777));
#197960=CARTESIAN_POINT('Ctrl Pts',(-16.6169353534846,19.2131362265077,
8.89032085944812));
#197961=CARTESIAN_POINT('Ctrl Pts',(-16.6174160277454,19.1431772098436,
8.8948421801714));
#197962=CARTESIAN_POINT('Ctrl Pts',(-16.6197932752915,19.0899272909105,
8.89822896713506));
#197963=CARTESIAN_POINT('Ctrl Pts',(-16.6248948323449,19.0281329449414,
8.90205384845788));
#197964=CARTESIAN_POINT('Ctrl Pts',(-16.6256656088748,19.019450869866,8.90258880433776));
#197965=CARTESIAN_POINT('Ctrl Pts',(-16.6269139357158,19.0063114350199,
8.90339445884502));
#197966=CARTESIAN_POINT('Ctrl Pts',(-16.6273520469587,19.0018505468898,
8.9036672919615));
#197967=CARTESIAN_POINT('Ctrl Pts',(-16.6281639264406,18.9938453722729,
8.90415561825538));
#197968=CARTESIAN_POINT('Ctrl Pts',(-16.6285324777938,18.9903006240027,
8.9043713992682));
#197969=CARTESIAN_POINT('Ctrl Pts',(-16.6293528007749,18.9825998185874,
8.90483918419298));
#197970=CARTESIAN_POINT('Ctrl Pts',(-16.6298079303377,18.9784441771552,
8.90509099685626));
#197971=CARTESIAN_POINT('Ctrl Pts',(-16.6311210653119,18.9667738933941,
8.90579648380971));
#197972=CARTESIAN_POINT('Ctrl Pts',(-16.6320070464334,18.9592623743418,
8.9062486107759));
#197973=CARTESIAN_POINT('Ctrl Pts',(-16.6375471916381,18.9143618234692,
8.90894037907243));
#197974=CARTESIAN_POINT('Ctrl Pts',(-16.6431588843496,18.877095208706,8.91112949011558));
#197975=CARTESIAN_POINT('Ctrl Pts',(-16.6649107936157,18.7548967700036,
8.91821704310322));
#197976=CARTESIAN_POINT('Ctrl Pts',(-16.6852577460059,18.6707983339279,
8.92295149499236));
#197977=CARTESIAN_POINT('Ctrl Pts',(-16.7625567222436,18.4196853984783,
8.93724930263314));
#197978=CARTESIAN_POINT('Ctrl Pts',(-16.8352561405136,18.2583550030579,
8.94672307059035));
#197979=CARTESIAN_POINT('Ctrl Pts',(-16.9390550078285,18.088330232005,8.95829925095575));
#197980=CARTESIAN_POINT('Ctrl Pts',(-16.9513216341481,18.0689524018888,
8.95964285881243));
#197981=CARTESIAN_POINT('Ctrl Pts',(-16.969131358301,18.0418042828294,8.96156167622395));
#197982=CARTESIAN_POINT('Ctrl Pts',(-16.9744161734379,18.0338658953712,
8.96212725255675));
#197983=CARTESIAN_POINT('Ctrl Pts',(-16.9830934919021,18.0210205956828,
8.96304988220527));
#197984=CARTESIAN_POINT('Ctrl Pts',(-16.9864534535734,18.016091781872,8.9634057032543));
#197985=CARTESIAN_POINT('Ctrl Pts',(-16.9935329185366,18.0058004608563,
8.96415247412125));
#197986=CARTESIAN_POINT('Ctrl Pts',(-16.9972564722743,18.0004408282812,
8.96454357572377));
#197987=CARTESIAN_POINT('Ctrl Pts',(-17.0061786955254,17.9877241967286,
8.96547680424103));
#197988=CARTESIAN_POINT('Ctrl Pts',(-17.0113996273458,17.9803830395787,
8.96601978149938));
#197989=CARTESIAN_POINT('Ctrl Pts',(-17.0291710971178,17.9557292513476,
8.96785776217277));
#197990=CARTESIAN_POINT('Ctrl Pts',(-17.0419367201608,17.9385739530716,
8.96916106564162));
#197991=CARTESIAN_POINT('Ctrl Pts',(-17.1130192831018,17.8460100314751,
8.97632986409577));
#197992=CARTESIAN_POINT('Ctrl Pts',(-17.1761113462918,17.7744225395055,
8.9823847662244));
#197993=CARTESIAN_POINT('Ctrl Pts',(-17.3649871583612,17.5872384093068,
8.99966511063359));
#197994=CARTESIAN_POINT('Ctrl Pts',(-17.500235715532,17.4822373117944,9.01117699066875));
#197995=CARTESIAN_POINT('Ctrl Pts',(-17.6780757781581,17.3757731528818,
9.02440467292287));
#197996=CARTESIAN_POINT('Ctrl Pts',(-17.7100233243319,17.3577580611091,
9.02671101795702));
#197997=CARTESIAN_POINT('Ctrl Pts',(-17.7487283094343,17.3372391839079,
9.0294086543798));
#197998=CARTESIAN_POINT('Ctrl Pts',(-17.7550487046079,17.3339293394465,
9.02984615095221));
#197999=CARTESIAN_POINT('Ctrl Pts',(-17.7653917042542,17.3285794014119,
9.03055702819858));
#198000=CARTESIAN_POINT('Ctrl Pts',(-17.7694042494542,17.3265201302546,
9.03083157517174));
#198001=CARTESIAN_POINT('Ctrl Pts',(-17.7766009793685,17.3228557178617,
9.03132173881997));
#198002=CARTESIAN_POINT('Ctrl Pts',(-17.7797826548772,17.3212457901225,
9.03153765288808));
#198003=CARTESIAN_POINT('Ctrl Pts',(-17.7866846432542,17.3177752598759,
9.03200432479047));
#198004=CARTESIAN_POINT('Ctrl Pts',(-17.7904063647455,17.3159175865058,
9.03225489893297));
#198005=CARTESIAN_POINT('Ctrl Pts',(-17.8008246586814,17.3107556621284,
9.0329534257104));
#198006=CARTESIAN_POINT('Ctrl Pts',(-17.8075333504167,17.3074758177955,
9.03339987971469));
#198007=CARTESIAN_POINT('Ctrl Pts',(-17.8467272179401,17.2885704330329,
9.03598950609465));
#198008=CARTESIAN_POINT('Ctrl Pts',(-17.879591988789,17.2737401492536,9.03808650695643));
#198009=CARTESIAN_POINT('Ctrl Pts',(-17.9867534853252,17.2286413910437,
9.04473680285233));
#198010=CARTESIAN_POINT('Ctrl Pts',(-18.0624000274753,17.2017517584273,
9.04914838643406));
#198011=CARTESIAN_POINT('Ctrl Pts',(-18.3174041456543,17.1271243204877,
9.06363240847603));
#198012=CARTESIAN_POINT('Ctrl Pts',(-18.5014653802449,17.0986525905144,
9.07355317091278));
#198013=CARTESIAN_POINT('Ctrl Pts',(-18.7089948933894,17.0940320884639,
9.08562592997281));
#198014=CARTESIAN_POINT('Ctrl Pts',(-18.7311173724334,17.0938863918305,
9.08692273217236));
#198015=CARTESIAN_POINT('Ctrl Pts',(-18.7616984633517,17.0941642979843,
9.08873050711022));
#198016=CARTESIAN_POINT('Ctrl Pts',(-18.7701588174278,17.0942919117261,
9.08923223288706));
#198017=CARTESIAN_POINT('Ctrl Pts',(-18.7846953954136,17.0945983540511,
9.09009713397423));
#198018=CARTESIAN_POINT('Ctrl Pts',(-18.7907720744447,17.0947526419464,
9.09045953758247));
#198019=CARTESIAN_POINT('Ctrl Pts',(-18.8032939124053,17.0951245450867,
9.09120811123557));
#198020=CARTESIAN_POINT('Ctrl Pts',(-18.8097389038583,17.0953454431273,
9.09159438038085));
#198021=CARTESIAN_POINT('Ctrl Pts',(-18.8247274460454,17.0959277428672,
9.09249501089743));
#198022=CARTESIAN_POINT('Ctrl Pts',(-18.8332699718761,17.0963114669789,
9.09301006703614));
#198023=CARTESIAN_POINT('Ctrl Pts',(-18.8605757342882,17.0977038404696,
9.09466214790892));
#198024=CARTESIAN_POINT('Ctrl Pts',(-18.879327559702,17.0989105276866,9.09580535420733));
#198025=CARTESIAN_POINT('Ctrl Pts',(-18.9727481865047,17.1061721504019,
9.10154549134328));
#198026=CARTESIAN_POINT('Ctrl Pts',(-19.0470671003556,17.1159372733713,
9.10625747982172));
#198027=CARTESIAN_POINT('Ctrl Pts',(-19.2277700331182,17.1495105884135,
9.11806559652373));
#198028=CARTESIAN_POINT('Ctrl Pts',(-19.333132455298,17.1776322855539,9.12526207470022));
#198029=CARTESIAN_POINT('Ctrl Pts',(-19.5489466401678,17.2534709350268,
9.14037430552462));
#198030=CARTESIAN_POINT('Ctrl Pts',(-19.6584722050729,17.3027505745684,
9.14826221120722));
#198031=CARTESIAN_POINT('Ctrl Pts',(-19.7715535833672,17.3656648203867,
9.15625475703304));
#198032=CARTESIAN_POINT('Ctrl Pts',(-19.7798294055048,17.3703424474378,
9.15683869334073));
#198033=CARTESIAN_POINT('Ctrl Pts',(-19.7920477901601,17.3773574846551,
9.15769901278247));
#198034=CARTESIAN_POINT('Ctrl Pts',(-19.7960145901564,17.3796521325673,
9.15797803905649));
#198035=CARTESIAN_POINT('Ctrl Pts',(-19.8029605202583,17.3837002557399,
9.15846607718493));
#198036=CARTESIAN_POINT('Ctrl Pts',(-19.8059428341996,17.3854481628643,
9.15867544418998));
#198037=CARTESIAN_POINT('Ctrl Pts',(-19.8123456343186,17.3892218862082,
9.15912454741573));
#198038=CARTESIAN_POINT('Ctrl Pts',(-19.8157646904125,17.3912500286798,
9.15936412924731));
#198039=CARTESIAN_POINT('Ctrl Pts',(-19.8228158807722,17.3954596043279,
9.15985777752131));
#198040=CARTESIAN_POINT('Ctrl Pts',(-19.8264472234304,17.3976423366422,
9.16011175914375));
#198041=CARTESIAN_POINT('Ctrl Pts',(-19.8355735642533,17.4031653741656,
9.16074951296143));
#198042=CARTESIAN_POINT('Ctrl Pts',(-19.8410599837193,17.4065198680463,
9.16113239711954));
#198043=CARTESIAN_POINT('Ctrl Pts',(-19.8566518707262,17.4161509008407,
9.16221931258732));
#198044=CARTESIAN_POINT('Ctrl Pts',(-19.8667200032386,17.4224877916183,
9.16291971426939));
#198045=CARTESIAN_POINT('Ctrl Pts',(-19.9004526476336,17.44411825938,9.16526333451959));
#198046=CARTESIAN_POINT('Ctrl Pts',(-19.9238660135968,17.4597998731897,
9.16688494411293));
#198047=CARTESIAN_POINT('Ctrl Pts',(-20.1096085667809,17.5896507172134,
9.17976728332988));
#198048=CARTESIAN_POINT('Ctrl Pts',(-20.2554714790839,17.7256674728927,
9.19008536896605));
#198049=CARTESIAN_POINT('Ctrl Pts',(-20.4259994360632,17.9365909473618,
9.20524794634643));
#198050=CARTESIAN_POINT('Ctrl Pts',(-20.4687833597732,17.9954731225062,
9.20939667530289));
#198051=CARTESIAN_POINT('Ctrl Pts',(-20.5155582447735,18.0673614571342,
9.21442962601142));
#198052=CARTESIAN_POINT('Ctrl Pts',(-20.5225657501326,18.0783520218739,
9.21519815903774));
#198053=CARTESIAN_POINT('Ctrl Pts',(-20.533800983204,18.0963376253222,9.21645467177886));
#198054=CARTESIAN_POINT('Ctrl Pts',(-20.5380905460369,18.1032937720209,
9.21694036383617));
#198055=CARTESIAN_POINT('Ctrl Pts',(-20.5456657214597,18.1157387370824,
9.21780887901529));
#198056=CARTESIAN_POINT('Ctrl Pts',(-20.5489669522373,18.1212179661699,
9.21819112311947));
#198057=CARTESIAN_POINT('Ctrl Pts',(-20.5558791164178,18.1328089791901,
9.21899947937157));
#198058=CARTESIAN_POINT('Ctrl Pts',(-20.5594842373245,18.1389241213593,
9.21942579725972));
#198059=CARTESIAN_POINT('Ctrl Pts',(-20.568957764628,18.1551798116322,9.22055872609264));
#198060=CARTESIAN_POINT('Ctrl Pts',(-20.5747728000763,18.1653510350095,
9.22126725643068));
#198061=CARTESIAN_POINT('Ctrl Pts',(-20.601608681013,18.2132079908139,9.22459978666674));
#198062=CARTESIAN_POINT('Ctrl Pts',(-20.6215572963592,18.2514802743453,
9.22726173152773));
#198063=CARTESIAN_POINT('Ctrl Pts',(-20.6735197136441,18.3590730335041,
9.2347418326464));
#198064=CARTESIAN_POINT('Ctrl Pts',(-20.7029724481655,18.4295514923801,
9.23964015626457));
#198065=CARTESIAN_POINT('Ctrl Pts',(-20.7868720819469,18.6653977969546,
9.25596369974907));
#198066=CARTESIAN_POINT('Ctrl Pts',(-20.8247559190743,18.8358935776873,
9.26771398111092));
#198067=CARTESIAN_POINT('Ctrl Pts',(-20.8438467744343,19.0351570450412,
9.28035994964475));
#198068=CARTESIAN_POINT('Ctrl Pts',(-20.8458598063493,19.0612586913657,
9.28199395121779));
#198069=CARTESIAN_POINT('Ctrl Pts',(-20.8477953023107,19.0943509189102,
9.28403153909177));
#198070=CARTESIAN_POINT('Ctrl Pts',(-20.8481679339001,19.101311629713,9.28445822647419));
#198071=CARTESIAN_POINT('Ctrl Pts',(-20.8487046766269,19.1123599294185,
9.28513232332365));
#198072=CARTESIAN_POINT('Ctrl Pts',(-20.8488913285337,19.1164463008669,
9.28538096266836));
#198073=CARTESIAN_POINT('Ctrl Pts',(-20.8492163340703,19.1240447614429,
9.28584199273702));
#198074=CARTESIAN_POINT('Ctrl Pts',(-20.8493577841925,19.1275566150248,
9.28605454922297));
#198075=CARTESIAN_POINT('Ctrl Pts',(-20.8496218268837,19.1345448797432,
9.28647649266277));
#198076=CARTESIAN_POINT('Ctrl Pts',(-20.8497445966673,19.138021223141,9.28668588806037));
#198077=CARTESIAN_POINT('Ctrl Pts',(-20.8500062528851,19.1459868452829,
9.28716457379975));
#198078=CARTESIAN_POINT('Ctrl Pts',(-20.8501394227778,19.1504763126595,
9.28743354980515));
#198079=CARTESIAN_POINT('Ctrl Pts',(-20.8504746952607,19.1631387302945,
9.28818997906115));
#198080=CARTESIAN_POINT('Ctrl Pts',(-20.8506437465519,19.1713125745779,
9.28867567321112));
#198081=CARTESIAN_POINT('Ctrl Pts',(-20.850918614115,19.1897759511114,9.28976732408507));
#198082=CARTESIAN_POINT('Ctrl Pts',(-20.8509967709457,19.2000657272674,
9.29037188547692));
#198083=CARTESIAN_POINT('Ctrl Pts',(-20.8509999019989,19.2103558441126,
9.29097300469246));
#198084=CARTESIAN_POINT('Ctrl Pts',(-20.8509999014157,19.2103539304217,
9.29097289290007));
#198085=CARTESIAN_POINT('Ctrl Pts',(-20.8510612394758,19.4113426033819,
9.30271408510573));
#198086=CARTESIAN_POINT('Ctrl Pts',(-20.8225007204989,19.6113597274272,
9.31315832230768));
#198087=CARTESIAN_POINT('Ctrl Pts',(-20.7530794884102,19.8491047828837,
9.32683241854603));
#198088=CARTESIAN_POINT('Ctrl Pts',(-20.7385514545259,19.8933713334306,
9.32943048944104));
#198089=CARTESIAN_POINT('Ctrl Pts',(-20.7225805876262,19.9371103542273,
9.33206810105871));
#198090=CARTESIAN_POINT('Origin',(-18.734,19.211,0.));
#198091=CARTESIAN_POINT('',(-20.7225806064498,19.9371103026755,10.3555828687981));
#198092=CARTESIAN_POINT('',(-20.7225805927058,19.9371103403161,10.1325349747556));
#198093=CARTESIAN_POINT('',(-20.7225806064498,19.9371103026755,0.));
#198094=CARTESIAN_POINT('',(-20.8533536084667,19.2099228989533,10.3109437268627));
#198095=CARTESIAN_POINT('Ctrl Pts',(-20.8509997268492,19.2099245835976,
10.3109437563769));
#198096=CARTESIAN_POINT('Ctrl Pts',(-20.8510361522909,19.2816295063777,
10.3152783077138));
#198097=CARTESIAN_POINT('Ctrl Pts',(-20.8474252680846,19.3534823809604,
10.3196128590508));
#198098=CARTESIAN_POINT('Ctrl Pts',(-20.8401482596367,19.4250759407999,
10.3239474103877));
#198099=CARTESIAN_POINT('Ctrl Pts',(-20.8328800282355,19.496583149219,10.3282767336752));
#198100=CARTESIAN_POINT('Ctrl Pts',(-20.8219544852716,19.5678311749355,
10.3326060569628));
#198101=CARTESIAN_POINT('Ctrl Pts',(-20.8074048164028,19.6384125259253,
10.3369353802504));
#198102=CARTESIAN_POINT('Ctrl Pts',(-20.7928691087884,19.7089261499988,
10.3412605493001));
#198103=CARTESIAN_POINT('Ctrl Pts',(-20.774716275487,19.7787738864939,10.3455857183499));
#198104=CARTESIAN_POINT('Ctrl Pts',(-20.7530311027341,19.8475551085275,
10.3499108873996));
#198105=CARTESIAN_POINT('Ctrl Pts',(-20.7435518665807,19.8776214332925,
10.3518015478658));
#198106=CARTESIAN_POINT('Ctrl Pts',(-20.7333983238929,19.9074840833062,
10.353692208332));
#198107=CARTESIAN_POINT('Ctrl Pts',(-20.7225806064498,19.9371103026755,
10.3555828687981));
#198108=CARTESIAN_POINT('Ctrl Pts',(-20.7242505210392,19.9377358132316,
9.55561791545399));
#198109=CARTESIAN_POINT('Ctrl Pts',(-20.5136267421919,20.4984180581842,
9.59172752760294));
#198110=CARTESIAN_POINT('Ctrl Pts',(-19.5197099108043,21.5302730444029,
9.67022907531242));
#198111=CARTESIAN_POINT('Ctrl Pts',(-17.2597752658646,21.2341144066335,
9.79112255858229));
#198112=CARTESIAN_POINT('Ctrl Pts',(-16.2349110611132,19.0664837566254,
9.91829836526376));
#198113=CARTESIAN_POINT('Ctrl Pts',(-17.5028058468379,17.0314377902239,
10.0454741719452));
#198114=CARTESIAN_POINT('Ctrl Pts',(-19.9002448515612,16.9960048724045,
10.1726499786266));
#198115=CARTESIAN_POINT('Ctrl Pts',(-20.8239162838523,18.3853146252952,
10.2611398283041));
#198116=CARTESIAN_POINT('Ctrl Pts',(-20.8542040821902,19.1485339254976,
10.307237742421));
#198117=CARTESIAN_POINT('Ctrl Pts',(-20.853822977789,19.2099225630314,10.3109437209775));
#198118=CARTESIAN_POINT('Ctrl Pts',(-20.7225805876262,19.9371103542273,
9.33206810105871));
#198119=CARTESIAN_POINT('Ctrl Pts',(-20.7083723124747,19.9760222083078,
9.33441461811644));
#198120=CARTESIAN_POINT('Ctrl Pts',(-20.6930221015738,20.0145165505172,
9.33679237043968));
#198121=CARTESIAN_POINT('Ctrl Pts',(-20.6684009468031,20.0713499495902,
9.3404023341193));
#198122=CARTESIAN_POINT('Ctrl Pts',(-20.6599812476126,20.0900365459304,
9.34160569950588));
#198123=CARTESIAN_POINT('Ctrl Pts',(-20.6475367889476,20.1166182362245,
9.34334237469629));
#198124=CARTESIAN_POINT('Ctrl Pts',(-20.6437315509185,20.1246152539405,
9.34386811257265));
#198125=CARTESIAN_POINT('Ctrl Pts',(-20.6370470770801,20.1384389791352,
9.34478268475076));
#198126=CARTESIAN_POINT('Ctrl Pts',(-20.6341909611294,20.1442767796274,
9.34517071080896));
#198127=CARTESIAN_POINT('Ctrl Pts',(-20.6286470866176,20.155477315503,9.34591869353401));
#198128=CARTESIAN_POINT('Ctrl Pts',(-20.6259633238204,20.1608419671164,
9.34627850748558));
#198129=CARTESIAN_POINT('Ctrl Pts',(-20.6188715784058,20.1748685554156,
9.34722341538004));
#198130=CARTESIAN_POINT('Ctrl Pts',(-20.6144267200328,20.1835115962596,
9.34780980218194));
#198131=CARTESIAN_POINT('Ctrl Pts',(-20.5987863506719,20.2134162090647,
9.34985330554818));
#198132=CARTESIAN_POINT('Ctrl Pts',(-20.587288806225,20.2345169348483,9.35132107029404));
#198133=CARTESIAN_POINT('Ctrl Pts',(-20.503433765002,20.3823636704645,9.36179375158657));
#198134=CARTESIAN_POINT('Ctrl Pts',(-20.4185109819538,20.5015028249208,
9.37126617387904));
#198135=CARTESIAN_POINT('Ctrl Pts',(-20.2315226373376,20.7136136358815,
9.38992783241288));
#198136=CARTESIAN_POINT('Ctrl Pts',(-20.1312641727334,20.8072707252901,
9.39904492515672));
#198137=CARTESIAN_POINT('Ctrl Pts',(-20.0125804369365,20.8983299731808,
9.4084127902312));
#198138=CARTESIAN_POINT('Ctrl Pts',(-20.0024322113572,20.9059720098676,
9.40920324599229));
#198139=CARTESIAN_POINT('Ctrl Pts',(-19.9867977229504,20.9175263694816,
9.41040421042433));
#198140=CARTESIAN_POINT('Ctrl Pts',(-19.9813607329896,20.9215044837379,
9.41081878247207));
#198141=CARTESIAN_POINT('Ctrl Pts',(-19.9723708079735,20.9280165357094,
9.41149909799248));
#198142=CARTESIAN_POINT('Ctrl Pts',(-19.9688289086725,20.9305655291434,
9.41176582084513));
#198143=CARTESIAN_POINT('Ctrl Pts',(-19.9619672203779,20.9354715368968,
9.41227997022959));
#198144=CARTESIAN_POINT('Ctrl Pts',(-19.9586484668834,20.9378299595197,
9.4125274910382));
#198145=CARTESIAN_POINT('Ctrl Pts',(-19.9553132045175,20.9401856628517,
9.41277506997446));
#198146=CARTESIAN_POINT('Ctrl Pts',(-19.95530351068,20.9401925095089,9.41277578954511));
#198147=CARTESIAN_POINT('Ctrl Pts',(-19.9552840886592,20.9402062268364,
9.41277723121601));
#198148=CARTESIAN_POINT('Ctrl Pts',(-19.9552743605407,20.9402130974602,
9.41277795331139));
#198149=CARTESIAN_POINT('Ctrl Pts',(-19.9552548697881,20.9402268628383,
9.41277940004412));
#198150=CARTESIAN_POINT('Ctrl Pts',(-19.9552451069065,20.9402337577667,
9.41278012469979));
#198151=CARTESIAN_POINT('Ctrl Pts',(-19.9552249130926,20.9402480191705,
9.41278162357678));
#198152=CARTESIAN_POINT('Ctrl Pts',(-19.9552144826606,20.9402553852751,
9.41278239775954));
#198153=CARTESIAN_POINT('Ctrl Pts',(-19.9551934538178,20.9402702358281,
9.41278395856987));
#198154=CARTESIAN_POINT('Ctrl Pts',(-19.9551828549229,20.9402777206137,
9.41278474523301));
#198155=CARTESIAN_POINT('Ctrl Pts',(-19.9551614854613,20.9402928111225,
9.41278633127706));
#198156=CARTESIAN_POINT('Ctrl Pts',(-19.9551507150833,20.9403004167077,
9.41278713064358));
#198157=CARTESIAN_POINT('Ctrl Pts',(-19.9551289992166,20.9403157512299,
9.41278874234848));
#198158=CARTESIAN_POINT('Ctrl Pts',(-19.9551180532273,20.9403234805154,
9.41278955472362));
#198159=CARTESIAN_POINT('Ctrl Pts',(-19.9550959816806,20.9403390655707,
9.41279119277532));
#198160=CARTESIAN_POINT('Ctrl Pts',(-19.9550848569857,20.9403469207263,
9.41279201838747));
#198161=CARTESIAN_POINT('Ctrl Pts',(-19.9550624244507,20.9403627600322,
9.41279368317742));
#198162=CARTESIAN_POINT('Ctrl Pts',(-19.9550511163289,20.940370744376,9.41279452237571));
#198163=CARTESIAN_POINT('Ctrl Pts',(-19.9550283129778,20.9403868448397,
9.41279621463067));
#198164=CARTESIAN_POINT('Ctrl Pts',(-19.9550168179877,20.9403949607852,
9.41279706766915));
#198165=CARTESIAN_POINT('Ctrl Pts',(-19.9549936369887,20.9404113271972,
9.41279878789342));
#198166=CARTESIAN_POINT('Ctrl Pts',(-19.9549819506578,20.9404195778851,
9.41279965510262));
#198167=CARTESIAN_POINT('Ctrl Pts',(-19.9549583829434,20.9404362166127,
9.41280140396625));
#198168=CARTESIAN_POINT('Ctrl Pts',(-19.9549465012232,20.940444604884,9.41280228564519));
#198169=CARTESIAN_POINT('Ctrl Pts',(-19.9549225377146,20.9404615223009,
9.41280406381898));
#198170=CARTESIAN_POINT('Ctrl Pts',(-19.9549104565878,20.9404700509732,
9.41280496026424));
#198171=CARTESIAN_POINT('Ctrl Pts',(-19.9548860899369,20.9404872522296,
9.41280676829041));
#198172=CARTESIAN_POINT('Ctrl Pts',(-19.9548738043449,20.9404959248551,
9.41280767987582));
#198173=CARTESIAN_POINT('Ctrl Pts',(-19.9548490244136,20.9405134170692,
9.41280951850347));
#198174=CARTESIAN_POINT('Ctrl Pts',(-19.9548365299727,20.9405222367226,
9.4128104455527));
#198175=CARTESIAN_POINT('Ctrl Pts',(-19.9548113274381,20.940540026435,9.41281231547029));
#198176=CARTESIAN_POINT('Ctrl Pts',(-19.9547986194878,20.9405489963856,
9.41281325832745));
#198177=CARTESIAN_POINT('Ctrl Pts',(-19.9547729853794,20.9405670898864,
9.41281516019715));
#198178=CARTESIAN_POINT('Ctrl Pts',(-19.9547600587298,20.9405762137762,
9.41281611924557));
#198179=CARTESIAN_POINT('Ctrl Pts',(-19.9547339820759,20.940594618766,9.41281805387785));
#198180=CARTESIAN_POINT('Ctrl Pts',(-19.9547208320502,20.9406038998735,
9.41281902946268));
#198181=CARTESIAN_POINT('Ctrl Pts',(-19.9518702664365,20.9426157412384,
9.41303050559343));
#198182=CARTESIAN_POINT('Ctrl Pts',(-19.9490279680172,20.9446112881187,
9.41324051485031));
#198183=CARTESIAN_POINT('Ctrl Pts',(-19.9424087524699,20.949234292255,9.41372762670196));
#198184=CARTESIAN_POINT('Ctrl Pts',(-19.9386281761675,20.9518564346082,
9.41400436526241));
#198185=CARTESIAN_POINT('Ctrl Pts',(-19.9269336087204,20.9599112467264,
9.41485596276838));
#198186=CARTESIAN_POINT('Ctrl Pts',(-19.9189910658487,20.9653025182226,
9.41542808190676));
#198187=CARTESIAN_POINT('Ctrl Pts',(-19.8165021515012,21.0338567104904,
9.42273437345601));
#198188=CARTESIAN_POINT('Ctrl Pts',(-19.717038601259,21.0893662932825,9.42900134393215));
#198189=CARTESIAN_POINT('Ctrl Pts',(-19.5099110397039,21.1839779160608,
9.44141177246223));
#198190=CARTESIAN_POINT('Ctrl Pts',(-19.4025860162462,21.2228826377151,
9.44753907605117));
#198191=CARTESIAN_POINT('Ctrl Pts',(-19.2395033767298,21.2674998371823,
9.45694036405629));
#198192=CARTESIAN_POINT('Ctrl Pts',(-19.1858102519556,21.2799591816438,
9.46004745135552));
#198193=CARTESIAN_POINT('Ctrl Pts',(-19.0980015922924,21.2967537267562,
9.46519081550471));
#198194=CARTESIAN_POINT('Ctrl Pts',(-19.0641581510429,21.3023778153729,
9.46718771769038));
#198195=CARTESIAN_POINT('Ctrl Pts',(-19.0194921664403,21.3086892159295,
9.46984812507602));
#198196=CARTESIAN_POINT('Ctrl Pts',(-19.0087787071528,21.3101194533097,
9.47048810736266));
#198197=CARTESIAN_POINT('Ctrl Pts',(-18.9912106985769,21.3123279706189,
9.47154078471046));
#198198=CARTESIAN_POINT('Ctrl Pts',(-18.9843623827013,21.3131549084605,
9.47195193865683));
#198199=CARTESIAN_POINT('Ctrl Pts',(-18.9710961970775,21.3146910620382,
9.47275000413827));
#198200=CARTESIAN_POINT('Ctrl Pts',(-18.9646788765133,21.3154044159015,
9.4731367803345));
#198201=CARTESIAN_POINT('Ctrl Pts',(-18.9498510711551,21.3169840458204,
9.47403217588533));
#198202=CARTESIAN_POINT('Ctrl Pts',(-18.9414385017158,21.3178293122451,
9.47454145144701));
#198203=CARTESIAN_POINT('Ctrl Pts',(-18.9187937407615,21.3199676381122,
9.4759158264876));
#198204=CARTESIAN_POINT('Ctrl Pts',(-18.9045533366357,21.3211670002328,
9.4767838544749));
#198205=CARTESIAN_POINT('Ctrl Pts',(-18.7737124064208,21.3308536736132,
9.48479486767219));
#198206=CARTESIAN_POINT('Ctrl Pts',(-18.6566272837034,21.3298115341273,
9.4922399577738));
#198207=CARTESIAN_POINT('Ctrl Pts',(-18.3780207271946,21.30420470784,9.51051549157705));
#198208=CARTESIAN_POINT('Ctrl Pts',(-18.2180663795343,21.2706212740284,
9.52148645629154));
#198209=CARTESIAN_POINT('Ctrl Pts',(-18.0329148996013,21.2088016788044,
9.53388734209194));
#198210=CARTESIAN_POINT('Ctrl Pts',(-18.0025197840609,21.1978741336953,
9.53591104784495));
#198211=CARTESIAN_POINT('Ctrl Pts',(-17.9656436128781,21.1836554847918,
9.53834131470093));
#198212=CARTESIAN_POINT('Ctrl Pts',(-17.9589156906172,21.1810217044809,
9.53878367693989));
#198213=CARTESIAN_POINT('Ctrl Pts',(-17.9483851120989,21.1768370000413,
9.53947429480328));
#198214=CARTESIAN_POINT('Ctrl Pts',(-17.9445733340599,21.1753093958406,
9.53972391409476));
#198215=CARTESIAN_POINT('Ctrl Pts',(-17.9374538901133,21.1724321442594,
9.54018942343491));
#198216=CARTESIAN_POINT('Ctrl Pts',(-17.9341452321789,21.1710852308843,
9.54040546773772));
#198217=CARTESIAN_POINT('Ctrl Pts',(-17.9265965685278,21.1679899673576,
9.54089771428285));
#198218=CARTESIAN_POINT('Ctrl Pts',(-17.922358832866,21.1662362134057,9.54117358570328));
#198219=CARTESIAN_POINT('Ctrl Pts',(-17.9093381078825,21.1607980608227,
9.54201986875329));
#198220=CARTESIAN_POINT('Ctrl Pts',(-17.9005741171114,21.1570680922558,
9.54258758981504));
#198221=CARTESIAN_POINT('Ctrl Pts',(-17.782929025579,21.1060576408512,9.55018678117345));
#198222=CARTESIAN_POINT('Ctrl Pts',(-17.6781704763533,21.0497527415101,
9.55670838499721));
#198223=CARTESIAN_POINT('Ctrl Pts',(-17.4871215863486,20.9253279009855,
9.56912064420152));
#198224=CARTESIAN_POINT('Ctrl Pts',(-17.4003237687817,20.8587052971729,
9.57500415806185));
#198225=CARTESIAN_POINT('Ctrl Pts',(-17.2781503546985,20.7489257189789,
9.58413785601873));
#198226=CARTESIAN_POINT('Ctrl Pts',(-17.238692224888,20.7105891845749,9.58723927556134));
#198227=CARTESIAN_POINT('Ctrl Pts',(-17.1771518333463,20.6459516725265,
9.59237409329115));
#198228=CARTESIAN_POINT('Ctrl Pts',(-17.1541371778341,20.6205729083274,
9.59436828818859));
#198229=CARTESIAN_POINT('Ctrl Pts',(-17.1246885345662,20.5864716693302,
9.59702559973078));
#198230=CARTESIAN_POINT('Ctrl Pts',(-17.1176905695215,20.5782415749621,
9.59766526328236));
#198231=CARTESIAN_POINT('Ctrl Pts',(-17.1063287045608,20.5646700931405,
9.59871754990777));
#198232=CARTESIAN_POINT('Ctrl Pts',(-17.1019273197589,20.5593602381188,
9.59912863411235));
#198233=CARTESIAN_POINT('Ctrl Pts',(-17.0934554419456,20.5490374622768,
9.5999266597221));
#198234=CARTESIAN_POINT('Ctrl Pts',(-17.0893817791442,20.5440272328854,
9.60031346629392));
#198235=CARTESIAN_POINT('Ctrl Pts',(-17.0800254800757,20.5324116782775,
9.60120907135326));
#198236=CARTESIAN_POINT('Ctrl Pts',(-17.0747594054637,20.5257932089295,
9.60171852701432));
#198237=CARTESIAN_POINT('Ctrl Pts',(-17.0606963242318,20.5078995045333,
9.60309370329275));
#198238=CARTESIAN_POINT('Ctrl Pts',(-17.0519737926135,20.4965665436334,
9.60396235773285));
#198239=CARTESIAN_POINT('Ctrl Pts',(-16.972516591875,20.3911367566103,9.61202351569985));
#198240=CARTESIAN_POINT('Ctrl Pts',(-16.9096424763334,20.2913972480126,
9.61952253163762));
#198241=CARTESIAN_POINT('Ctrl Pts',(-16.7799847257009,20.0418221704587,
9.63789912037959));
#198242=CARTESIAN_POINT('Ctrl Pts',(-16.7216567648856,19.8884335690771,
9.64891538407312));
#198243=CARTESIAN_POINT('Ctrl Pts',(-16.6739757242247,19.6998239156768,
9.66125913182953));
#198244=CARTESIAN_POINT('Ctrl Pts',(-16.6670422527242,19.6696226584634,
9.66319881259296));
#198245=CARTESIAN_POINT('Ctrl Pts',(-16.6593309330688,19.6322934057461,
9.66554221773797));
#198246=CARTESIAN_POINT('Ctrl Pts',(-16.6579233039985,19.6253011304167,
9.6659788494655));
#198247=CARTESIAN_POINT('Ctrl Pts',(-16.6557648778657,19.6142920442681,
9.66666252092505));
#198248=CARTESIAN_POINT('Ctrl Pts',(-16.6549903411732,19.6102800207873,
9.66691088031755));
#198249=CARTESIAN_POINT('Ctrl Pts',(-16.6535598290674,19.6027530849862,
9.66737531317241));
#198250=CARTESIAN_POINT('Ctrl Pts',(-16.6529011500223,19.5992387941174,
9.66759153326132));
#198251=CARTESIAN_POINT('Ctrl Pts',(-16.6514121583734,19.5911818072088,
9.6680858421601));
#198252=CARTESIAN_POINT('Ctrl Pts',(-16.6505878051263,19.5866380595754,
9.66836358952008));
#198253=CARTESIAN_POINT('Ctrl Pts',(-16.6480803550525,19.5725550628477,
9.66922139368315));
#198254=CARTESIAN_POINT('Ctrl Pts',(-16.6464478293761,19.5630067778102,
9.66979865259885));
#198255=CARTESIAN_POINT('Ctrl Pts',(-16.6279609211413,19.4502263873174,
9.67656949773241));
#198256=CARTESIAN_POINT('Ctrl Pts',(-16.6187119317562,19.3458784281049,
9.68236860186208));
#198257=CARTESIAN_POINT('Ctrl Pts',(-16.6148005740982,19.0722859228046,
9.69731859862332));
#198258=CARTESIAN_POINT('Ctrl Pts',(-16.6326252356836,18.9036416198706,
9.70632881182754));
#198259=CARTESIAN_POINT('Ctrl Pts',(-16.6796530836691,18.6980637473473,
9.71838536827981));
#198260=CARTESIAN_POINT('Ctrl Pts',(-16.6902075756455,18.6575047175167,
9.72081453095264));
#198261=CARTESIAN_POINT('Ctrl Pts',(-16.7052112877906,18.6061529768218,
9.72396600025222));
#198262=CARTESIAN_POINT('Ctrl Pts',(-16.7085559212137,18.5950455894642,
9.7246522392589));
#198263=CARTESIAN_POINT('Ctrl Pts',(-16.7140865696057,18.5772107913768,
9.72576171661946));
#198264=CARTESIAN_POINT('Ctrl Pts',(-16.7162153410324,18.5704657734164,
9.72618307494958));
#198265=CARTESIAN_POINT('Ctrl Pts',(-16.7203354362771,18.5576356161355,
9.72698798052912));
#198266=CARTESIAN_POINT('Ctrl Pts',(-16.7223206461291,18.5515485847238,
9.72737132265636));
#198267=CARTESIAN_POINT('Ctrl Pts',(-16.7269175487943,18.537667540411,9.72824891014382));
#198268=CARTESIAN_POINT('Ctrl Pts',(-16.7295470723675,18.5298795811279,
9.72874374036002));
#198269=CARTESIAN_POINT('Ctrl Pts',(-16.7365144843569,18.5096337411346,
9.73003662642503));
#198270=CARTESIAN_POINT('Ctrl Pts',(-16.7409235266807,18.497200887219,9.73083703059558));
#198271=CARTESIAN_POINT('Ctrl Pts',(-16.7716690078757,18.4130094243426,
9.7363018639495));
#198272=CARTESIAN_POINT('Ctrl Pts',(-16.8017561228273,18.3426894667636,
9.74109128645236));
#198273=CARTESIAN_POINT('Ctrl Pts',(-16.921780172379,18.0994722372349,9.75846999541262));
#198274=CARTESIAN_POINT('Ctrl Pts',(-17.0316660862533,17.9375479685287,
9.77166726323247));
#198275=CARTESIAN_POINT('Ctrl Pts',(-17.1902366627887,17.7617778206229,
9.78683301440995));
#198276=CARTESIAN_POINT('Ctrl Pts',(-17.2192701516351,17.7314581116134,
9.78947996192508));
#198277=CARTESIAN_POINT('Ctrl Pts',(-17.2547430210394,17.6965533927764,
9.79254374545519));
#198278=CARTESIAN_POINT('Ctrl Pts',(-17.2603282817907,17.6911179627308,
9.7930213352587));
#198279=CARTESIAN_POINT('Ctrl Pts',(-17.2689913127958,17.6827799764446,
9.79375453963165));
#198280=CARTESIAN_POINT('Ctrl Pts',(-17.2720479121388,17.6798556607885,
9.79401180162807));
#198281=CARTESIAN_POINT('Ctrl Pts',(-17.2776933699718,17.6744868446462,
9.79448428436337));
#198282=CARTESIAN_POINT('Ctrl Pts',(-17.2802796124028,17.6720397301195,
9.79469970453727));
#198283=CARTESIAN_POINT('Ctrl Pts',(-17.2860908403172,17.6665688399374,
9.79518145660487));
#198284=CARTESIAN_POINT('Ctrl Pts',(-17.2893191197814,17.6635486443792,
9.79544751356641));
#198285=CARTESIAN_POINT('Ctrl Pts',(-17.2975687555384,17.6558790691032,
9.79612349225951));
#198286=CARTESIAN_POINT('Ctrl Pts',(-17.3026032819286,17.6512438433648,
9.79653235653453));
#198287=CARTESIAN_POINT('Ctrl Pts',(-17.3315053871257,17.6248918288508,
9.79885930004098));
#198288=CARTESIAN_POINT('Ctrl Pts',(-17.3558459481913,17.6036973111419,
9.80074054842719));
#198289=CARTESIAN_POINT('Ctrl Pts',(-17.3954616522374,17.5707639069678,
9.80369742715779));
#198290=CARTESIAN_POINT('Ctrl Pts',(-17.410427767966,17.5586634915258,9.80479154979167));
#198291=CARTESIAN_POINT('Ctrl Pts',(-17.426697316939,17.5458721375866,9.80595906110082));
#198292=CARTESIAN_POINT('Ctrl Pts',(-17.4278383477558,17.5449769384711,
9.8060408276413));
#198293=CARTESIAN_POINT('Ctrl Pts',(-17.4470195008386,17.5299601252104,
9.80741344965776));
#198294=CARTESIAN_POINT('Ctrl Pts',(-17.4652872283598,17.5161307361346,
9.80869245245463));
#198295=CARTESIAN_POINT('Ctrl Pts',(-17.5206370878767,17.4756251646983,
9.81249557890216));
#198296=CARTESIAN_POINT('Ctrl Pts',(-17.5583623569115,17.449849312523,9.8149932263107));
#198297=CARTESIAN_POINT('Ctrl Pts',(-17.6891293853963,17.3665781944157,
9.82343367022865));
#198298=CARTESIAN_POINT('Ctrl Pts',(-17.7857771714591,17.3150783291671,
9.82932176592834));
#198299=CARTESIAN_POINT('Ctrl Pts',(-17.9364617660584,17.2492000869357,
9.83846611489902));
#198300=CARTESIAN_POINT('Ctrl Pts',(-17.9877967539146,17.2291054004682,
9.84157363858167));
#198301=CARTESIAN_POINT('Ctrl Pts',(-18.0722656972139,17.1997879945636,
9.84671766068652));
#198302=CARTESIAN_POINT('Ctrl Pts',(-18.1049439105122,17.1893288452427,
9.84871477123229));
#198303=CARTESIAN_POINT('Ctrl Pts',(-18.1482320468893,17.1766249760926,
9.85137541687025));
#198304=CARTESIAN_POINT('Ctrl Pts',(-18.1586265732511,17.1736607435132,
9.85201542367111));
#198305=CARTESIAN_POINT('Ctrl Pts',(-18.1756912036971,17.1689353896586,
9.85306813107032));
#198306=CARTESIAN_POINT('Ctrl Pts',(-18.1823481036325,17.1671270175619,
9.85347929038108));
#198307=CARTESIAN_POINT('Ctrl Pts',(-18.1952528750725,17.163689025558,9.85427735893401));
#198308=CARTESIAN_POINT('Ctrl Pts',(-18.2014996045733,17.1620553892002,
9.85466413279845));
#198309=CARTESIAN_POINT('Ctrl Pts',(-18.2159429947749,17.1583486848286,
9.85555951225615));
#198310=CARTESIAN_POINT('Ctrl Pts',(-18.2241447551176,17.1562961020224,
9.85606877398238));
#198311=CARTESIAN_POINT('Ctrl Pts',(-18.2462414748078,17.1509065982363,
9.85744308747781));
#198312=CARTESIAN_POINT('Ctrl Pts',(-18.2601581038214,17.1476611900619,
9.85831106734732));
#198313=CARTESIAN_POINT('Ctrl Pts',(-18.3881653251675,17.119172758855,9.86631840861463));
#198314=CARTESIAN_POINT('Ctrl Pts',(-18.5041113482054,17.1032793757705,
9.87375955380936));
#198315=CARTESIAN_POINT('Ctrl Pts',(-18.7832498985648,17.0883266666903,
9.89201887790245));
#198316=CARTESIAN_POINT('Ctrl Pts',(-18.9461968238054,17.0983854555601,
9.90297711145388));
#198317=CARTESIAN_POINT('Ctrl Pts',(-19.1383850972074,17.1327270232927,
9.91538262627974));
#198318=CARTESIAN_POINT('Ctrl Pts',(-19.1702539013258,17.139182277625,9.917420184744));
#198319=CARTESIAN_POINT('Ctrl Pts',(-19.2090239435011,17.1479697852639,
9.91986473493801));
#198320=CARTESIAN_POINT('Ctrl Pts',(-19.2160764507605,17.1496063663328,
9.92030801579544));
#198321=CARTESIAN_POINT('Ctrl Pts',(-19.2271190429344,17.1522286433133,
9.92099974674368));
#198322=CARTESIAN_POINT('Ctrl Pts',(-19.2311148119395,17.1531898158401,
9.92124956761185));
#198323=CARTESIAN_POINT('Ctrl Pts',(-19.2385781685672,17.1550081152537,
9.92171525135607));
#198324=CARTESIAN_POINT('Ctrl Pts',(-19.2420463477369,17.1558623727062,
9.92193126970113));
#198325=CARTESIAN_POINT('Ctrl Pts',(-19.2499579841591,17.157832362697,9.92242319618484));
#198326=CARTESIAN_POINT('Ctrl Pts',(-19.2543999835046,17.1589537416619,
9.92269877515916));
#198327=CARTESIAN_POINT('Ctrl Pts',(-19.2680410713539,17.1624445650132,
9.92354327015164));
#198328=CARTESIAN_POINT('Ctrl Pts',(-19.2772280261641,17.164861550309,9.92410951206675));
#198329=CARTESIAN_POINT('Ctrl Pts',(-19.3595520277177,17.1871136227094,
9.92916361140246));
#198330=CARTESIAN_POINT('Ctrl Pts',(-19.4315996383471,17.210802823055,9.93344569392556));
#198331=CARTESIAN_POINT('Ctrl Pts',(-19.5420512036803,17.2538161595377,
9.94000648320762));
#198332=CARTESIAN_POINT('Ctrl Pts',(-19.5813960228866,17.2705269907126,
9.94234263424595));
#198333=CARTESIAN_POINT('Ctrl Pts',(-19.7194906226425,17.3341813100814,
9.95062123118651));
#198334=CARTESIAN_POINT('Ctrl Pts',(-19.8150773194542,17.3875661227974,
9.95650793123038));
#198335=CARTESIAN_POINT('Ctrl Pts',(-19.9519738974235,17.4785849429644,
9.96564903557837));
#198336=CARTESIAN_POINT('Ctrl Pts',(-19.9966274390109,17.5108548148603,
9.96875469954442));
#198337=CARTESIAN_POINT('Ctrl Pts',(-20.0669593696601,17.5659819849045,
9.97389591760056));
#198338=CARTESIAN_POINT('Ctrl Pts',(-20.0934295913258,17.5877883868564,
9.97589214010261));
#198339=CARTESIAN_POINT('Ctrl Pts',(-20.1275293159034,17.6172993255093,
9.97855177028231));
#198340=CARTESIAN_POINT('Ctrl Pts',(-20.1356467557165,17.6244338463876,
9.9791916725856));
#198341=CARTESIAN_POINT('Ctrl Pts',(-20.1488551336826,17.6362233396075,
9.98024425188442));
#198342=CARTESIAN_POINT('Ctrl Pts',(-20.1539786396014,17.6408416510526,
9.98065538832868));
#198343=CARTESIAN_POINT('Ctrl Pts',(-20.1638543627909,17.6498314652345,
9.98145344379378));
#198344=CARTESIAN_POINT('Ctrl Pts',(-20.168609335561,17.6541998376084,9.98184022760254));
#198345=CARTESIAN_POINT('Ctrl Pts',(-20.1795448213011,17.6643388644299,
9.98273567568082));
#198346=CARTESIAN_POINT('Ctrl Pts',(-20.1857108628382,17.6701249024822,
9.98324499639986));
#198347=CARTESIAN_POINT('Ctrl Pts',(-20.2022061769968,17.6857905324228,
9.98461957232397));
#198348=CARTESIAN_POINT('Ctrl Pts',(-20.2124701921566,17.6957379192579,
9.98548775736936));
#198349=CARTESIAN_POINT('Ctrl Pts',(-20.3058953903506,17.7881340820861,
9.99351092039735));
#198350=CARTESIAN_POINT('Ctrl Pts',(-20.382168567715,17.8772327582584,10.0009690673243));
#198351=CARTESIAN_POINT('Ctrl Pts',(-20.5463777362288,18.1047806390244,
10.0193001576771));
#198352=CARTESIAN_POINT('Ctrl Pts',(-20.6263877479788,18.2480341934771,
10.0303152960732));
#198353=CARTESIAN_POINT('Ctrl Pts',(-20.7012121906667,18.4282095779477,
10.042700831961));
#198354=CARTESIAN_POINT('Ctrl Pts',(-20.7126617678792,18.4576192839732,
10.0446771660736));
#198355=CARTESIAN_POINT('Ctrl Pts',(-20.7259025049934,18.4940168294528,
10.0470585100492));
#198356=CARTESIAN_POINT('Ctrl Pts',(-20.7283205544069,18.5007704695581,
10.0474976755916));
#198357=CARTESIAN_POINT('Ctrl Pts',(-20.7320650318759,18.5113987578401,
10.0481844190689));
#198358=CARTESIAN_POINT('Ctrl Pts',(-20.7334145988123,18.5152651134591,
10.0484333360482));
#198359=CARTESIAN_POINT('Ctrl Pts',(-20.7359210084947,18.5225132174356,
10.0488982423822));
#198360=CARTESIAN_POINT('Ctrl Pts',(-20.7370804931179,18.5258939408191,
10.0491143817466));
#198361=CARTESIAN_POINT('Ctrl Pts',(-20.7397139287311,18.5336361169858,
10.0496077645352));
#198362=CARTESIAN_POINT('Ctrl Pts',(-20.7411822155883,18.5379994440847,
10.0498846712711));
#198363=CARTESIAN_POINT('Ctrl Pts',(-20.7456726562695,18.5514891608176,
10.050737301678));
#198364=CARTESIAN_POINT('Ctrl Pts',(-20.748646934659,18.5606315201919,10.0513102759193));
#198365=CARTESIAN_POINT('Ctrl Pts',(-20.7774526056146,18.6512687556419,
10.0569455155612));
#198366=CARTESIAN_POINT('Ctrl Pts',(-20.7983905411972,18.7342475906723,
10.0617452393583));
#198367=CARTESIAN_POINT('Ctrl Pts',(-20.8385991839127,18.9472314285597,
10.0736796187252));
#198368=CARTESIAN_POINT('Ctrl Pts',(-20.8509009165662,19.0781722963637,
10.0806786689208));
#198369=CARTESIAN_POINT('Ctrl Pts',(-20.8510686215296,19.3016470631716,
10.0930379618485));
#198370=CARTESIAN_POINT('Ctrl Pts',(-20.8451100151077,19.3937783280465,
10.0982491651107));
#198371=CARTESIAN_POINT('Ctrl Pts',(-20.8313804909468,19.4988780661773,
10.1044628226863));
#198372=CARTESIAN_POINT('Ctrl Pts',(-20.8294631854275,19.5125173791607,
10.1052743194174));
#198373=CARTESIAN_POINT('Ctrl Pts',(-20.8261768233744,19.5343482583805,
10.1065817984235));
#198374=CARTESIAN_POINT('Ctrl Pts',(-20.8248923986009,19.5425523049788,
10.1070751037696));
#198375=CARTESIAN_POINT('Ctrl Pts',(-20.8225273356179,19.5570981837842,
10.1079532951721));
#198376=CARTESIAN_POINT('Ctrl Pts',(-20.8214659898445,19.5634430794814,
10.1083375644673));
#198377=CARTESIAN_POINT('Ctrl Pts',(-20.8191956392426,19.5766455016435,
10.1091396978766));
#198378=CARTESIAN_POINT('Ctrl Pts',(-20.8179816887034,19.5835020887657,
10.1095577151611));
#198379=CARTESIAN_POINT('Ctrl Pts',(-20.8147441170231,19.6012771145112,
10.1106451675106));
#198380=CARTESIAN_POINT('Ctrl Pts',(-20.8126683965908,19.6121857378977,
10.1113162553442));
#198381=CARTESIAN_POINT('Ctrl Pts',(-20.8033102345472,19.6593426322595,
10.1142337296146));
#198382=CARTESIAN_POINT('Ctrl Pts',(-20.7951650779569,19.695411203176,10.1165074902027));
#198383=CARTESIAN_POINT('Ctrl Pts',(-20.7710540774191,19.790515584671,10.1226195362212));
#198384=CARTESIAN_POINT('Ctrl Pts',(-20.7534685869628,19.8491012118838,
10.126506512534));
#198385=CARTESIAN_POINT('Ctrl Pts',(-20.7298520717044,19.916959144821,10.131146365902));
#198386=CARTESIAN_POINT('Ctrl Pts',(-20.7262541603358,19.9270496306836,
10.1318399254289));
#198387=CARTESIAN_POINT('Ctrl Pts',(-20.7225805927058,19.9371103403161,
10.1325349747556));
#198388=CARTESIAN_POINT('Origin',(-18.734,19.211,0.));
#198389=CARTESIAN_POINT('',(-20.7225806899004,19.9371100741315,11.1558808822554));
#198390=CARTESIAN_POINT('',(-20.7225806064498,19.9371103026755,10.9336112484111));
#198391=CARTESIAN_POINT('',(-20.7225806064498,19.9371103026755,0.));
#198392=CARTESIAN_POINT('',(-20.8509995968923,19.2096935705332,11.1109437209282));
#198393=CARTESIAN_POINT('Ctrl Pts',(-20.7225806899004,19.9371100741315,
11.1558808822554));
#198394=CARTESIAN_POINT('Ctrl Pts',(-20.7445653673935,19.8769011516913,
11.1523876403128));
#198395=CARTESIAN_POINT('Ctrl Pts',(-20.763823629495,19.8156719423086,11.1488667470025));
#198396=CARTESIAN_POINT('Ctrl Pts',(-20.7906145513329,19.7146376108668,
11.1430184534343));
#198397=CARTESIAN_POINT('Ctrl Pts',(-20.799831825771,19.6753843887736,11.1407374126506));
#198398=CARTESIAN_POINT('Ctrl Pts',(-20.8091426808549,19.6299377205522,
11.1380746344932));
#198399=CARTESIAN_POINT('Ctrl Pts',(-20.810337188784,19.6239767996495,11.137724952832));
#198400=CARTESIAN_POINT('Ctrl Pts',(-20.8121465849177,19.6147410968476,
11.1371824640975));
#198401=CARTESIAN_POINT('Ctrl Pts',(-20.812779451429,19.6114698413517,11.1369901805635));
#198402=CARTESIAN_POINT('Ctrl Pts',(-20.8188276074304,19.5798065618939,
11.1351276632203));
#198403=CARTESIAN_POINT('Ctrl Pts',(-20.8236684176471,19.5513090037321,
11.1334407399127));
#198404=CARTESIAN_POINT('Ctrl Pts',(-20.829467698782,19.5123536362169,11.1311168047545));
#198405=CARTESIAN_POINT('Ctrl Pts',(-20.8309342155032,19.5019738485889,
11.1304958634879));
#198406=CARTESIAN_POINT('Ctrl Pts',(-20.8331379328417,19.4854935205726,
11.1295070910953));
#198407=CARTESIAN_POINT('Ctrl Pts',(-20.8339257795473,19.4793998381151,
11.1291408638761));
#198408=CARTESIAN_POINT('Ctrl Pts',(-20.8354516395268,19.4671797870958,
11.1284051599387));
#198409=CARTESIAN_POINT('Ctrl Pts',(-20.8361894175406,19.4610534505192,
11.128035679647));
#198410=CARTESIAN_POINT('Ctrl Pts',(-20.837616391639,19.4487513233087,11.1272924070941));
#198411=CARTESIAN_POINT('Ctrl Pts',(-20.8383052007998,19.4425755503276,
11.1269186065157));
#198412=CARTESIAN_POINT('Ctrl Pts',(-20.839817318421,19.4284539825217,11.1260623031829));
#198413=CARTESIAN_POINT('Ctrl Pts',(-20.8406228594108,19.4205064164719,
11.1255792453081));
#198414=CARTESIAN_POINT('Ctrl Pts',(-20.8425678109608,19.4001706896508,
11.124340258937));
#198415=CARTESIAN_POINT('Ctrl Pts',(-20.8436430281583,19.3877768271365,
11.1235823280557));
#198416=CARTESIAN_POINT('Ctrl Pts',(-20.8489047513553,19.3202149734588,
11.1194348915391));
#198417=CARTESIAN_POINT('Ctrl Pts',(-20.851036203119,19.2649135578119,11.1159820029749));
#198418=CARTESIAN_POINT('Ctrl Pts',(-20.8509995348902,19.2095966915971,
11.1124693680802));
#198419=CARTESIAN_POINT('Ctrl Pts',(-20.7225806064498,19.9371103026755,
10.3555828687981));
#198420=CARTESIAN_POINT('Ctrl Pts',(-20.6978477139366,20.0048456731998,
10.3599055461406));
#198421=CARTESIAN_POINT('Ctrl Pts',(-20.6696397182687,20.071343807373,10.3642282234831));
#198422=CARTESIAN_POINT('Ctrl Pts',(-20.6381130431754,20.1362256583177,
10.3685509008256));
#198423=CARTESIAN_POINT('Ctrl Pts',(-20.6065863063599,20.2011076362865,
10.3728735866309));
#198424=CARTESIAN_POINT('Ctrl Pts',(-20.5717410957585,20.2643728810197,
10.3771962724362));
#198425=CARTESIAN_POINT('Ctrl Pts',(-20.5337806062108,20.3256653172623,
10.3815189582415));
#198426=CARTESIAN_POINT('Ctrl Pts',(-20.495782105661,20.3870191275007,10.3858459724846));
#198427=CARTESIAN_POINT('Ctrl Pts',(-20.4546623619949,20.4463957658043,
10.3901729867278));
#198428=CARTESIAN_POINT('Ctrl Pts',(-20.4106683247005,20.5034675349679,
10.3945000009709));
#198429=CARTESIAN_POINT('Ctrl Pts',(-20.3666497254667,20.560571167389,10.3988294309929));
#198430=CARTESIAN_POINT('Ctrl Pts',(-20.3197539628617,20.6153669959171,
10.4031588610148));
#198431=CARTESIAN_POINT('Ctrl Pts',(-20.2702669159773,20.6675620353674,
10.4074882910367));
#198432=CARTESIAN_POINT('Ctrl Pts',(-20.2206957718595,20.719845773956,10.4118250783998));
#198433=CARTESIAN_POINT('Ctrl Pts',(-20.1685249152318,20.7695195646485,
10.4161618657629));
#198434=CARTESIAN_POINT('Ctrl Pts',(-20.114074862226,20.816329366408,10.420498653126));
#198435=CARTESIAN_POINT('Ctrl Pts',(-20.0868592195423,20.839726200175,10.4226662994138));
#198436=CARTESIAN_POINT('Ctrl Pts',(-20.0590746522195,20.8624081912211,
10.4248339457017));
#198437=CARTESIAN_POINT('Ctrl Pts',(-20.0307638001157,20.8843477363386,
10.4270015919895));
#198438=CARTESIAN_POINT('Ctrl Pts',(-19.9734509743371,20.9287624124624,
10.4313898009204));
#198439=CARTESIAN_POINT('Ctrl Pts',(-19.9137418045025,20.9703158984433,
10.4357780098513));
#198440=CARTESIAN_POINT('Ctrl Pts',(-19.8519537768691,21.0087397900653,
10.4401662187821));
#198441=CARTESIAN_POINT('Ctrl Pts',(-19.7902574529134,21.0471066542614,
10.4445479148834));
#198442=CARTESIAN_POINT('Ctrl Pts',(-19.7264888022841,21.0823528921034,
10.4489296109847));
#198443=CARTESIAN_POINT('Ctrl Pts',(-19.6609970987611,21.1142512653059,
10.4533113070859));
#198444=CARTESIAN_POINT('Ctrl Pts',(-19.5955823532016,21.1461121553814,
10.4576878543455));
#198445=CARTESIAN_POINT('Ctrl Pts',(-19.5284490083968,21.1746327855719,
10.4620644016052));
#198446=CARTESIAN_POINT('Ctrl Pts',(-19.4599724698909,21.199630929298,10.4664409488648));
#198447=CARTESIAN_POINT('Ctrl Pts',(-19.3915393582105,21.2246132195646,
10.4708147205818));
#198448=CARTESIAN_POINT('Ctrl Pts',(-19.3217651949909,21.2460772907209,
10.4751884922988));
#198449=CARTESIAN_POINT('Ctrl Pts',(-19.2510456730823,21.2638888844618,
10.4795622640157));
#198450=CARTESIAN_POINT('Ctrl Pts',(-19.1803476713616,21.281695058075,10.4839347047793));
#198451=CARTESIAN_POINT('Ctrl Pts',(-19.1087053495654,21.295850843123,10.4883071455428));
#198452=CARTESIAN_POINT('Ctrl Pts',(-19.0365282611626,21.3062722141044,
10.4926795863064));
#198453=CARTESIAN_POINT('Ctrl Pts',(-18.9643493271836,21.3166938515614,
10.4970521388737));
#198454=CARTESIAN_POINT('Ctrl Pts',(-18.8916360771621,21.3233808184121,
10.5014246914411));
#198455=CARTESIAN_POINT('Ctrl Pts',(-18.8188052520575,21.3263007042081,
10.5057972440084));
#198456=CARTESIAN_POINT('Ctrl Pts',(-18.7458988403756,21.3292236203718,
10.5101743345757));
#198457=CARTESIAN_POINT('Ctrl Pts',(-18.6728750930034,21.3283716302984,
10.5145514251431));
#198458=CARTESIAN_POINT('Ctrl Pts',(-18.6001519939633,21.3237644713219,
10.5189285157104));
#198459=CARTESIAN_POINT('Ctrl Pts',(-18.5273891781396,21.3191547962048,
10.5233079967693));
#198460=CARTESIAN_POINT('Ctrl Pts',(-18.4549278170834,21.3107859243705,
10.5276874778283));
#198461=CARTESIAN_POINT('Ctrl Pts',(-18.3831792948549,21.2987293485606,
10.5320669588872));
#198462=CARTESIAN_POINT('Ctrl Pts',(-18.3113035988522,21.2866514025511,
10.5364542025469));
#198463=CARTESIAN_POINT('Ctrl Pts',(-18.2401437361938,21.2708728040954,
10.5408414462066));
#198464=CARTESIAN_POINT('Ctrl Pts',(-18.1700988737775,21.2515157484923,
10.5452286898664));
#198465=CARTESIAN_POINT('Ctrl Pts',(-18.1224751168409,21.2383548159235,
10.5482115928012));
#198466=CARTESIAN_POINT('Ctrl Pts',(-18.0753664841794,21.2235407241658,
10.551194495736));
#198467=CARTESIAN_POINT('Ctrl Pts',(-18.0288930166915,21.2071245307068,
10.5541773986709));
#198468=CARTESIAN_POINT('Ctrl Pts',(-17.960524957276,21.1829743359732,10.5585656076018));
#198469=CARTESIAN_POINT('Ctrl Pts',(-17.8932656103902,21.1552604871605,
10.5629538165327));
#198470=CARTESIAN_POINT('Ctrl Pts',(-17.8275125107933,21.1241046578564,
10.5673420254636));
#198471=CARTESIAN_POINT('Ctrl Pts',(-17.7618569996982,21.0929950689686,
10.5717237215649));
#198472=CARTESIAN_POINT('Ctrl Pts',(-17.6977037303933,21.0584538454431,
10.5761054176661));
#198473=CARTESIAN_POINT('Ctrl Pts',(-17.6354328295881,21.0206516714808,
10.5804871137674));
#198474=CARTESIAN_POINT('Ctrl Pts',(-17.5732351020472,20.9828939180814,
10.5848636610271));
#198475=CARTESIAN_POINT('Ctrl Pts',(-17.5129157592863,20.9418830753682,
10.5892402082867));
#198476=CARTESIAN_POINT('Ctrl Pts',(-17.4548312249217,20.8978361642035,
10.5936167555463));
#198477=CARTESIAN_POINT('Ctrl Pts',(-17.3967835269247,20.8538171869497,
10.5979905272633));
#198478=CARTESIAN_POINT('Ctrl Pts',(-17.3409682086661,20.8067662523013,
10.6023642989803));
#198479=CARTESIAN_POINT('Ctrl Pts',(-17.2877123411685,20.7569434038514,
10.6067380706973));
#198480=CARTESIAN_POINT('Ctrl Pts',(-17.2344726796103,20.7071357166617,
10.6111105114608));
#198481=CARTESIAN_POINT('Ctrl Pts',(-17.1837912746023,20.654558119635,10.6154829522244));
#198482=CARTESIAN_POINT('Ctrl Pts',(-17.135960461819,20.5995095010155,10.6198553929879));
#198483=CARTESIAN_POINT('Ctrl Pts',(-17.0881284259965,20.5444594747966,
10.6242279455553));
#198484=CARTESIAN_POINT('Ctrl Pts',(-17.0431474419898,20.4869386669777,
10.6286004981226));
#198485=CARTESIAN_POINT('Ctrl Pts',(-17.0012703358341,20.4272799475941,
10.63297305069));
#198486=CARTESIAN_POINT('Ctrl Pts',(-16.9593497680381,20.3675593121413,
10.6373501412573));
#198487=CARTESIAN_POINT('Ctrl Pts',(-16.9205397874118,20.3056967307924,
10.6417272318246));
#198488=CARTESIAN_POINT('Ctrl Pts',(-16.8850500448046,20.2420543454071,
10.6461043223919));
#198489=CARTESIAN_POINT('Ctrl Pts',(-16.8495409199318,20.1783772025532,
10.6504838034509));
#198490=CARTESIAN_POINT('Ctrl Pts',(-16.8173558563405,20.1129187535682,
10.6548632845098));
#198491=CARTESIAN_POINT('Ctrl Pts',(-16.7886574143382,20.0460636050089,
10.6592427655688));
#198492=CARTESIAN_POINT('Ctrl Pts',(-16.75990810454,19.9790899561476,10.6636300092285));
#198493=CARTESIAN_POINT('Ctrl Pts',(-16.7346579248205,19.9107151168649,
10.6680172528882));
#198494=CARTESIAN_POINT('Ctrl Pts',(-16.7130201897423,19.8413408653503,
10.6724044965479));
#198495=CARTESIAN_POINT('Ctrl Pts',(-16.6983086148963,19.7941730592073,
10.6753873994827));
#198496=CARTESIAN_POINT('Ctrl Pts',(-16.68526591231,19.7465435673453,10.6783703024176));
#198497=CARTESIAN_POINT('Ctrl Pts',(-16.673914126578,19.6985809616125,10.6813532053524));
#198498=CARTESIAN_POINT('Ctrl Pts',(-16.6572142846389,19.6280222007594,
10.6857414142833));
#198499=CARTESIAN_POINT('Ctrl Pts',(-16.6441110368839,19.5564667533231,
10.6901296232142));
#198500=CARTESIAN_POINT('Ctrl Pts',(-16.6347172531062,19.4843147427305,
10.6945178321451));
#198501=CARTESIAN_POINT('Ctrl Pts',(-16.6253374112611,19.4122698176846,
10.6988995282463));
#198502=CARTESIAN_POINT('Ctrl Pts',(-16.6196561660671,19.3396305615062,
10.7032812243476));
#198503=CARTESIAN_POINT('Ctrl Pts',(-16.6177357545009,19.2668089887221,
10.7076629204489));
#198504=CARTESIAN_POINT('Ctrl Pts',(-16.6158175995711,19.1940729870813,
10.7120394677085));
#198505=CARTESIAN_POINT('Ctrl Pts',(-16.6176515119966,19.1211555742338,
10.7164160149681));
#198506=CARTESIAN_POINT('Ctrl Pts',(-16.6232479369201,19.0484739153123,
10.7207925622278));
#198507=CARTESIAN_POINT('Ctrl Pts',(-16.6288408126722,18.9758383500427,
10.7251663339447));
#198508=CARTESIAN_POINT('Ctrl Pts',(-16.6381914295875,18.9034387218191,
10.7295401056617));
#198509=CARTESIAN_POINT('Ctrl Pts',(-16.6512581694981,18.8316908022766,
10.7339138773787));
#198510=CARTESIAN_POINT('Ctrl Pts',(-16.6643209331558,18.7599647158668,
10.7382863181422));
#198511=CARTESIAN_POINT('Ctrl Pts',(-16.6810974883882,18.6888904187038,
10.7426587589058));
#198512=CARTESIAN_POINT('Ctrl Pts',(-16.701494753238,18.6188755013641,10.7470311996693));
#198513=CARTESIAN_POINT('Ctrl Pts',(-16.7218925396481,18.5488587937351,
10.7514037522367));
#198514=CARTESIAN_POINT('Ctrl Pts',(-16.7459110826477,18.4799019822764,
10.755776304804));
#198515=CARTESIAN_POINT('Ctrl Pts',(-16.7734073411523,18.4123978299098,
10.7601488573714));
#198516=CARTESIAN_POINT('Ctrl Pts',(-16.8009321363112,18.3448236191879,
10.7645259479387));
#198517=CARTESIAN_POINT('Ctrl Pts',(-16.8319416708364,18.2787055253263,
10.768903038506));
#198518=CARTESIAN_POINT('Ctrl Pts',(-16.8662449207624,18.2144158520314,
10.7732801290733));
#198519=CARTESIAN_POINT('Ctrl Pts',(-16.9005669049664,18.1500910677599,
10.7776596101323));
#198520=CARTESIAN_POINT('Ctrl Pts',(-16.9381859370547,18.0875971057585,
10.7820390911912));
#198521=CARTESIAN_POINT('Ctrl Pts',(-16.9788666145896,18.0272788337544,
10.7864185722502));
#198522=CARTESIAN_POINT('Ctrl Pts',(-17.0196193983523,17.9668536480182,
10.7908058159099));
#198523=CARTESIAN_POINT('Ctrl Pts',(-17.0634443742614,17.9086122391294,
10.7951930595696));
#198524=CARTESIAN_POINT('Ctrl Pts',(-17.1100650454662,17.8528673616163,
10.7995803032293));
#198525=CARTESIAN_POINT('Ctrl Pts',(-17.1417626095282,17.814966216471,10.8025632061641));
#198526=CARTESIAN_POINT('Ctrl Pts',(-17.1747517071182,17.7782184270681,
10.8055461090989));
#198527=CARTESIAN_POINT('Ctrl Pts',(-17.2089361619795,17.7427121229261,
10.8085290120338));
#198528=CARTESIAN_POINT('Ctrl Pts',(-17.259225605987,17.6904780796656,10.8129172209647));
#198529=CARTESIAN_POINT('Ctrl Pts',(-17.3122998738987,17.6407287153967,
10.8173054298956));
#198530=CARTESIAN_POINT('Ctrl Pts',(-17.3678836195123,17.5937755149754,
10.8216936388265));
#198531=CARTESIAN_POINT('Ctrl Pts',(-17.4233848696313,17.5468920008886,
10.8260753349277));
#198532=CARTESIAN_POINT('Ctrl Pts',(-17.4813878383957,17.5027967211001,
10.830457031029));
#198533=CARTESIAN_POINT('Ctrl Pts',(-17.5415797744861,17.461765022707,10.8348387271302));
#198534=CARTESIAN_POINT('Ctrl Pts',(-17.6017009802613,17.4207815398249,
10.8392152743899));
#198535=CARTESIAN_POINT('Ctrl Pts',(-17.6640056470483,17.3828547573656,
10.8435918216495));
#198536=CARTESIAN_POINT('Ctrl Pts',(-17.7281486587458,17.3482192616153,
10.8479683689091));
#198537=CARTESIAN_POINT('Ctrl Pts',(-17.7922509918775,17.313605731193,10.8523421406261));
#198538=CARTESIAN_POINT('Ctrl Pts',(-17.8581889333117,17.2822795746618,
10.8567159123431));
#198539=CARTESIAN_POINT('Ctrl Pts',(-17.9255903577758,17.2544308470287,
10.8610896840601));
#198540=CARTESIAN_POINT('Ctrl Pts',(-17.9929712717601,17.2265905938569,
10.8654621248236));
#198541=CARTESIAN_POINT('Ctrl Pts',(-18.0618143390775,17.2022258528362,
10.8698345655872));
#198542=CARTESIAN_POINT('Ctrl Pts',(-18.1317264570577,17.1814789778197,
10.8742070063507));
#198543=CARTESIAN_POINT('Ctrl Pts',(-18.2016403626988,17.1607315723032,
10.8785795589181));
#198544=CARTESIAN_POINT('Ctrl Pts',(-18.2726229102616,17.1436023517758,
10.8829521114854));
#198545=CARTESIAN_POINT('Ctrl Pts',(-18.3442664228591,17.1301836364424,
10.8873246640528));
#198546=CARTESIAN_POINT('Ctrl Pts',(-18.4159842897961,17.1167509946602,
10.8917017546201));
#198547=CARTESIAN_POINT('Ctrl Pts',(-18.4883640162146,17.1070366356522,
10.8960788451874));
#198548=CARTESIAN_POINT('Ctrl Pts',(-18.5609891559666,17.1010814594286,
10.9004559357548));
#198549=CARTESIAN_POINT('Ctrl Pts',(-18.6336539590027,17.0951230308623,
10.9048354168137));
#198550=CARTESIAN_POINT('Ctrl Pts',(-18.70656395973,17.092927887168,10.9092148978726));
#198551=CARTESIAN_POINT('Ctrl Pts',(-18.7793017600913,17.0944847625087,
10.9135943789316));
#198552=CARTESIAN_POINT('Ctrl Pts',(-18.8521684877156,17.0960443974006,
10.9179816225913));
#198553=CARTESIAN_POINT('Ctrl Pts',(-18.9248619239415,17.1013692966915,
10.922368866251));
#198554=CARTESIAN_POINT('Ctrl Pts',(-18.9969694292041,17.1103962583809,
10.9267561099107));
#198555=CARTESIAN_POINT('Ctrl Pts',(-19.04599558452,17.1165337224938,10.9297390128456));
#198556=CARTESIAN_POINT('Ctrl Pts',(-19.0947510327818,17.1243814515022,
10.9327219157804));
#198557=CARTESIAN_POINT('Ctrl Pts',(-19.1431096126277,17.1339062792316,
10.9357048187152));
#198558=CARTESIAN_POINT('Ctrl Pts',(-19.2142508990198,17.1479184462449,
10.9400930276461));
#198559=CARTESIAN_POINT('Ctrl Pts',(-19.2848103359499,17.1656171190662,
10.944481236577));
#198560=CARTESIAN_POINT('Ctrl Pts',(-19.3543769742706,17.1869393759586,
10.9488694455079));
#198561=CARTESIAN_POINT('Ctrl Pts',(-19.4238403641655,17.2082299870864,
10.9532511416092));
#198562=CARTESIAN_POINT('Ctrl Pts',(-19.4923134231172,17.2331333660321,
10.9576328377104));
#198563=CARTESIAN_POINT('Ctrl Pts',(-19.5593953414341,17.2615355785911,
10.9620145338117));
#198564=CARTESIAN_POINT('Ctrl Pts',(-19.6263984331584,17.2899044162902,
10.9663910810713));
#198565=CARTESIAN_POINT('Ctrl Pts',(-19.6920131895935,17.3217637331238,
10.970767628331));
#198566=CARTESIAN_POINT('Ctrl Pts',(-19.7558555559969,17.3569503181742,
10.9751441755906));
#198567=CARTESIAN_POINT('Ctrl Pts',(-19.8196574344994,17.3921145884038,
10.9795179473076));
#198568=CARTESIAN_POINT('Ctrl Pts',(-19.8816887317569,17.4306017078617,
10.9838917190246));
#198569=CARTESIAN_POINT('Ctrl Pts',(-19.941588217233,17.4722016512545,10.9882654907415));
#198570=CARTESIAN_POINT('Ctrl Pts',(-20.0014694750944,17.5137889356447,
10.9926379315051));
#198571=CARTESIAN_POINT('Ctrl Pts',(-20.0592198131158,17.5584868884064,
10.9970103722686));
#198572=CARTESIAN_POINT('Ctrl Pts',(-20.1145067552151,17.6060420258444,
11.0013828130322));
#198573=CARTESIAN_POINT('Ctrl Pts',(-20.1697951110076,17.6535983792726,
11.0057553655995));
#198574=CARTESIAN_POINT('Ctrl Pts',(-20.2226195814183,17.7040117463509,
11.0101279181669));
#198575=CARTESIAN_POINT('Ctrl Pts',(-20.2726818719981,17.7569893065096,
11.0145004707342));
#198576=CARTESIAN_POINT('Ctrl Pts',(-20.3227961191113,17.8100218487785,
11.0188775613015));
#198577=CARTESIAN_POINT('Ctrl Pts',(-20.3701421308266,17.8656235460727,
11.0232546518688));
#198578=CARTESIAN_POINT('Ctrl Pts',(-20.4144601023066,17.9234663714854,
11.0276317424362));
#198579=CARTESIAN_POINT('Ctrl Pts',(-20.4588022774757,17.9813407870121,
11.0320112234951));
#198580=CARTESIAN_POINT('Ctrl Pts',(-20.5001128464797,18.0414583697185,
11.036390704554));
#198581=CARTESIAN_POINT('Ctrl Pts',(-20.5381753524532,18.1034620559095,
11.040770185613));
#198582=CARTESIAN_POINT('Ctrl Pts',(-20.576305323963,18.165575643218,11.0451574292727));
#198583=CARTESIAN_POINT('Ctrl Pts',(-20.611175504632,18.2295815860898,11.0495446729324));
#198584=CARTESIAN_POINT('Ctrl Pts',(-20.6426156833706,18.2950987099081,
11.0539319165921));
#198585=CARTESIAN_POINT('Ctrl Pts',(-20.6639919753445,18.3396440408898,
11.056914819527));
#198586=CARTESIAN_POINT('Ctrl Pts',(-20.6837836766024,18.3848874840296,
11.0598977224618));
#198587=CARTESIAN_POINT('Ctrl Pts',(-20.7019503858964,18.4307050053664,
11.0628806253966));
#198588=CARTESIAN_POINT('Ctrl Pts',(-20.7321363776461,18.5068358719245,
11.0678370477142));
#198589=CARTESIAN_POINT('Ctrl Pts',(-20.7579328257801,18.5848010792849,
11.0727934700317));
#198590=CARTESIAN_POINT('Ctrl Pts',(-20.7791414399035,18.6641129085547,
11.0777498923493));
#198591=CARTESIAN_POINT('Ctrl Pts',(-20.8002681015216,18.7431182678655,
11.0826871624853));
#198592=CARTESIAN_POINT('Ctrl Pts',(-20.8168421753556,18.8234596442832,
11.0876244326214));
#198593=CARTESIAN_POINT('Ctrl Pts',(-20.8287143558564,18.904632953193,11.0925617027575));
#198594=CARTESIAN_POINT('Ctrl Pts',(-20.840509956428,18.9852826644165,11.097467125686));
#198595=CARTESIAN_POINT('Ctrl Pts',(-20.8476640072495,19.0667533747692,
11.1023725486145));
#198596=CARTESIAN_POINT('Ctrl Pts',(-20.8500781623712,19.1485323224719,
11.1072779715431));
#198597=CARTESIAN_POINT('Ctrl Pts',(-20.8506795164088,19.1689030517394,
11.1084998880048));
#198598=CARTESIAN_POINT('Ctrl Pts',(-20.8509870073137,19.1892928268125,
11.1097218044665));
#198599=CARTESIAN_POINT('Ctrl Pts',(-20.8509995968923,19.2096935705332,
11.1109437209282));
#198600=CARTESIAN_POINT('',(-20.8509995968923,19.2123064294671,10.8890562790718));
#198601=CARTESIAN_POINT('Ctrl Pts',(-20.7225805927058,19.9371103403161,
10.1325349747556));
#198602=CARTESIAN_POINT('Ctrl Pts',(-20.6722700068885,20.0748947086263,
10.1420538790795));
#198603=CARTESIAN_POINT('Ctrl Pts',(-20.6077708800263,20.2070921693553,
10.151890455237));
#198604=CARTESIAN_POINT('Ctrl Pts',(-20.4974383372554,20.3839378624421,
10.1654299576843));
#198605=CARTESIAN_POINT('Ctrl Pts',(-20.4624925057593,20.4348517776986,
10.1693726388878));
#198606=CARTESIAN_POINT('Ctrl Pts',(-20.4198757026397,20.4914669170025,
10.173746424394));
#198607=CARTESIAN_POINT('Ctrl Pts',(-20.4143358602232,20.4987281599882,
10.1743071704144));
#198608=CARTESIAN_POINT('Ctrl Pts',(-20.405991196218,20.5095202221887,10.1751399668579));
#198609=CARTESIAN_POINT('Ctrl Pts',(-20.403221888764,20.5130781906646,10.1754144254421));
#198610=CARTESIAN_POINT('Ctrl Pts',(-20.3982421237061,20.5194341281866,
10.1759044939734));
#198611=CARTESIAN_POINT('Ctrl Pts',(-20.3960359528224,20.5222353740848,
10.1761204008213));
#198612=CARTESIAN_POINT('Ctrl Pts',(-20.3912401647724,20.5282931893853,
10.1765871284904));
#198613=CARTESIAN_POINT('Ctrl Pts',(-20.3886480299972,20.5315476924542,
10.1768377652364));
#198614=CARTESIAN_POINT('Ctrl Pts',(-20.3813738080093,20.5406256504569,
10.1775366433218));
#198615=CARTESIAN_POINT('Ctrl Pts',(-20.3766704055904,20.5464320559437,
10.1779833835897));
#198616=CARTESIAN_POINT('Ctrl Pts',(-20.3490477356145,20.5801658143092,
10.1805780413002));
#198617=CARTESIAN_POINT('Ctrl Pts',(-20.3254458485314,20.6075295120245,
10.1826795773869));
#198618=CARTESIAN_POINT('Ctrl Pts',(-20.2470258197943,20.6938768565625,
10.1893509428739));
#198619=CARTESIAN_POINT('Ctrl Pts',(-20.1895377961755,20.7503448783542,
10.1937780257805));
#198620=CARTESIAN_POINT('Ctrl Pts',(-20.0272911806018,20.8924751985434,
10.205535102627));
#198621=CARTESIAN_POINT('Ctrl Pts',(-19.9173224873183,20.9715985056218,
10.2127866121133));
#198622=CARTESIAN_POINT('Ctrl Pts',(-19.7460918468844,21.0714664705331,
10.2239370092751));
#198623=CARTESIAN_POINT('Ctrl Pts',(-19.6902329837888,21.1007837892465,
10.2275506563067));
#198624=CARTESIAN_POINT('Ctrl Pts',(-19.6218463304284,21.1328672852451,
10.2319868157594));
#198625=CARTESIAN_POINT('Ctrl Pts',(-19.6104934947065,21.1380713822479,
10.2327235935239));
#198626=CARTESIAN_POINT('Ctrl Pts',(-19.5917883596035,21.1464462604983,
10.2339383599015));
#198627=CARTESIAN_POINT('Ctrl Pts',(-19.5844628406245,21.1496763657643,
10.2344143091388));
#198628=CARTESIAN_POINT('Ctrl Pts',(-19.5712677747777,21.1554054021022,
10.2352720590958));
#198629=CARTESIAN_POINT('Ctrl Pts',(-19.565404894644,21.1579195140505,10.2356533355446));
#198630=CARTESIAN_POINT('Ctrl Pts',(-19.5529028188346,21.1632138667234,
10.2364667493653));
#198631=CARTESIAN_POINT('Ctrl Pts',(-19.5462606410044,21.165986817655,10.2368991288974));
#198632=CARTESIAN_POINT('Ctrl Pts',(-19.528356405446,21.1733544137094,10.2380652907038));
#198633=CARTESIAN_POINT('Ctrl Pts',(-19.5170688042838,21.177885909746,10.2388011971044));
#198634=CARTESIAN_POINT('Ctrl Pts',(-19.4607287147891,21.1999422332628,
10.2424783379126));
#198635=CARTESIAN_POINT('Ctrl Pts',(-19.4151272682136,21.2160164281905,
10.2454677186487));
#198636=CARTESIAN_POINT('Ctrl Pts',(-19.282560450199,21.2577008790079,10.2542017717621));
#198637=CARTESIAN_POINT('Ctrl Pts',(-19.1944550767868,21.2793039049885,
10.2600638133215));
#198638=CARTESIAN_POINT('Ctrl Pts',(-18.9466759619437,21.323439323219,10.2765860700516));
#198639=CARTESIAN_POINT('Ctrl Pts',(-18.7853982408565,21.3334969258075,
10.2874121703723));
#198640=CARTESIAN_POINT('Ctrl Pts',(-18.6045529745864,21.3241334235593,
10.2987722432675));
#198641=CARTESIAN_POINT('Ctrl Pts',(-18.5845846127825,21.3228154529584,
10.3000151640786));
#198642=CARTESIAN_POINT('Ctrl Pts',(-18.5582752748694,21.3207039021706,
10.3016350769499));
#198643=CARTESIAN_POINT('Ctrl Pts',(-18.5519156706789,21.3201645344263,
10.3020252822205));
#198644=CARTESIAN_POINT('Ctrl Pts',(-18.5416547912929,21.3192475379835,
10.3026525440244));
#198645=CARTESIAN_POINT('Ctrl Pts',(-18.5377520124521,21.3188878264005,
10.3028905856347));
#198646=CARTESIAN_POINT('Ctrl Pts',(-18.5302461106706,21.3181749949476,
10.3033473220732));
#198647=CARTESIAN_POINT('Ctrl Pts',(-18.5266428913036,21.3178234706212,
10.3035661008765));
#198648=CARTESIAN_POINT('Ctrl Pts',(-18.5181207875851,21.3169699932925,
10.3040824415807));
#198649=CARTESIAN_POINT('Ctrl Pts',(-18.5132026915968,21.3164600439652,
10.3043795545946));
#198650=CARTESIAN_POINT('Ctrl Pts',(-18.4968956579324,21.3147114277419,
10.3053619562062));
#198651=CARTESIAN_POINT('Ctrl Pts',(-18.485514762443,21.3133975218965,10.3060431477741));
#198652=CARTESIAN_POINT('Ctrl Pts',(-18.4583813967461,21.3100416079543,
10.3076577749112));
#198653=CARTESIAN_POINT('Ctrl Pts',(-18.4426399379007,21.3079145503646,
10.3085869153626));
#198654=CARTESIAN_POINT('Ctrl Pts',(-18.3847298137794,21.2994247416996,
10.3119819533344));
#198655=CARTESIAN_POINT('Ctrl Pts',(-18.3427300801996,21.2919651269961,
10.3143990293684));
#198656=CARTESIAN_POINT('Ctrl Pts',(-18.1521714016529,21.2521457566835,
10.3252730197185));
#198657=CARTESIAN_POINT('Ctrl Pts',(-18.0071385216096,21.2051107556225,
10.3333207048918));
#198658=CARTESIAN_POINT('Ctrl Pts',(-17.7812050228889,21.1038807677603,
10.3469912183704));
#198659=CARTESIAN_POINT('Ctrl Pts',(-17.6967756912564,21.0589659910465,
10.3523802563669));
#198660=CARTESIAN_POINT('Ctrl Pts',(-17.6039048668715,21.0011860524091,
10.3587916159442));
#198661=CARTESIAN_POINT('Ctrl Pts',(-17.5922086031033,20.9937488618731,
10.3596081753665));
#198662=CARTESIAN_POINT('Ctrl Pts',(-17.573601717547,20.9816592579012,10.360922257278));
#198663=CARTESIAN_POINT('Ctrl Pts',(-17.5666439412484,20.9770798992629,
10.3614170590713));
#198664=CARTESIAN_POINT('Ctrl Pts',(-17.5543575432001,20.968889105883,10.3622969749089));
#198665=CARTESIAN_POINT('Ctrl Pts',(-17.5490179991131,20.9652941858845,
10.3626814638666));
#198666=CARTESIAN_POINT('Ctrl Pts',(-17.5379462395731,20.957766363201,10.3634831108117));
#198667=CARTESIAN_POINT('Ctrl Pts',(-17.5322168420308,20.9538294709666,
10.3639004172791));
#198668=CARTESIAN_POINT('Ctrl Pts',(-17.5174292233435,20.9435607315022,
10.3649839676944));
#198669=CARTESIAN_POINT('Ctrl Pts',(-17.5084010956056,20.9371861027277,
10.3656518422405));
#198670=CARTESIAN_POINT('Ctrl Pts',(-17.4697850913289,20.90946424837,10.3685363102943));
#198671=CARTESIAN_POINT('Ctrl Pts',(-17.4407033050697,20.8874258221909,
10.3707795165235));
#198672=CARTESIAN_POINT('Ctrl Pts',(-17.3653248046872,20.8271743133028,
10.3767886303896));
#198673=CARTESIAN_POINT('Ctrl Pts',(-17.3200613581114,20.787726887068,10.3806012202841));
#198674=CARTESIAN_POINT('Ctrl Pts',(-17.1553520348191,20.6313796017348,
10.3952543022437));
#198675=CARTESIAN_POINT('Ctrl Pts',(-17.0482235207344,20.5024171305579,
10.4065010679343));
#198676=CARTESIAN_POINT('Ctrl Pts',(-16.9463728577249,20.3452342862648,
10.4186131048079));
#198677=CARTESIAN_POINT('Ctrl Pts',(-16.9356159839769,20.3281003508967,
10.4199133111844));
#198678=CARTESIAN_POINT('Ctrl Pts',(-16.906553162828,20.2802999568463,10.4234804164344));
#198679=CARTESIAN_POINT('Ctrl Pts',(-16.8887740686995,20.2493188094764,
10.4257251613407));
#198680=CARTESIAN_POINT('Ctrl Pts',(-16.868421535263,20.2116777888174,10.428359848409));
#198681=CARTESIAN_POINT('Ctrl Pts',(-16.8650879914422,20.2054380084342,
10.4287936100046));
#198682=CARTESIAN_POINT('Ctrl Pts',(-16.8596890920909,20.1952092235228,
10.4294996437514));
#198683=CARTESIAN_POINT('Ctrl Pts',(-16.8576050739897,20.1912302064707,
10.4297730563891));
#198684=CARTESIAN_POINT('Ctrl Pts',(-16.8538899700927,20.1840816928529,
10.430262002301));
#198685=CARTESIAN_POINT('Ctrl Pts',(-16.8522542177986,20.1809146958789,
10.4304778266448));
#198686=CARTESIAN_POINT('Ctrl Pts',(-16.848720678445,20.1740307865896,10.430945227638));
#198687=CARTESIAN_POINT('Ctrl Pts',(-16.8468258868471,20.1703124014303,
10.4311966156227));
#198688=CARTESIAN_POINT('Ctrl Pts',(-16.8415429403344,20.1598687921114,
10.4318997135726));
#198689=CARTESIAN_POINT('Ctrl Pts',(-16.8381796162148,20.1531309800705,
10.4323498930077));
#198690=CARTESIAN_POINT('Ctrl Pts',(-16.8184564931481,20.1130859558023,
10.4350060078636));
#198691=CARTESIAN_POINT('Ctrl Pts',(-16.8029376883378,20.0793690030319,
10.4371629580768));
#198692=CARTESIAN_POINT('Ctrl Pts',(-16.7551226905858,19.9678532451521,
10.444095560181));
#198693=CARTESIAN_POINT('Ctrl Pts',(-16.7265791073742,19.8885292138496,
10.4487153085571));
#198694=CARTESIAN_POINT('Ctrl Pts',(-16.652240803465,19.6354862292233,10.4630752647893));
#198695=CARTESIAN_POINT('Ctrl Pts',(-16.6237589320657,19.457548301185,10.4727058102398));
#198696=CARTESIAN_POINT('Ctrl Pts',(-16.6173461289145,19.2554918041819,
10.4844566424849));
#198697=CARTESIAN_POINT('Ctrl Pts',(-16.6169910278957,19.2328193531069,
10.4857853182322));
#198698=CARTESIAN_POINT('Ctrl Pts',(-16.6170040011973,19.2006521637118,
10.4876864661778));
#198699=CARTESIAN_POINT('Ctrl Pts',(-16.6170716964181,19.1911583848314,
10.488249548472));
#198700=CARTESIAN_POINT('Ctrl Pts',(-16.6172857986382,19.1757086291063,
10.489169223374));
#198701=CARTESIAN_POINT('Ctrl Pts',(-16.6173934925153,19.1697521823283,
10.4895245996546));
#198702=CARTESIAN_POINT('Ctrl Pts',(-16.6176719965794,19.1572648832638,
10.4902713500743));
#198703=CARTESIAN_POINT('Ctrl Pts',(-16.6178478989413,19.1507342175656,
10.490662880035));
#198704=CARTESIAN_POINT('Ctrl Pts',(-16.6183394476929,19.1351629437227,
10.4915988261956));
#198705=CARTESIAN_POINT('Ctrl Pts',(-16.6186828158395,19.1261233947551,
10.4921441058168));
#198706=CARTESIAN_POINT('Ctrl Pts',(-16.6200426342039,19.0955005407325,
10.4939980398286));
#198707=CARTESIAN_POINT('Ctrl Pts',(-16.621331551719,19.0739312478338,10.4953151913678));
#198708=CARTESIAN_POINT('Ctrl Pts',(-16.6302341083521,18.9554439302184,
10.5026154383313));
#198709=CARTESIAN_POINT('Ctrl Pts',(-16.6441856191071,18.8591318388708,
10.5087958059423));
#198710=CARTESIAN_POINT('Ctrl Pts',(-16.6897931054439,18.6479397843144,
10.5228491338026));
#198711=CARTESIAN_POINT('Ctrl Pts',(-16.7246257532691,18.5340719590099,
10.5307724833707));
#198712=CARTESIAN_POINT('Ctrl Pts',(-16.780172889355,18.3954146033851,10.5405693270477));
#198713=CARTESIAN_POINT('Ctrl Pts',(-16.7921305131261,18.3673395680752,
10.5425599972482));
#198714=CARTESIAN_POINT('Ctrl Pts',(-16.8269256299967,18.2903080193825,
10.5480251827271));
#198715=CARTESIAN_POINT('Ctrl Pts',(-16.8510379405187,18.2419482316065,
10.551460127144));
#198716=CARTESIAN_POINT('Ctrl Pts',(-16.8811748334136,18.1868884918671,
10.5553323094483));
#198717=CARTESIAN_POINT('Ctrl Pts',(-16.8854212788035,18.1792431504343,
10.5558690833038));
#198718=CARTESIAN_POINT('Ctrl Pts',(-16.8919188084727,18.1677138306035,
10.5566769275715));
#198719=CARTESIAN_POINT('Ctrl Pts',(-16.8941350092539,18.1638104449919,
10.5569501494967));
#198720=CARTESIAN_POINT('Ctrl Pts',(-16.8981332843079,18.1568201736699,
10.5574388913103));
#198721=CARTESIAN_POINT('Ctrl Pts',(-16.8999107469432,18.153730726618,10.5576547012042));
#198722=CARTESIAN_POINT('Ctrl Pts',(-16.9037875130085,18.147031631927,10.5581222276757));
#198723=CARTESIAN_POINT('Ctrl Pts',(-16.905889689162,18.143423713312,10.5583737547417));
#198724=CARTESIAN_POINT('Ctrl Pts',(-16.9118183201517,18.1333173956787,
10.5590776348027));
#198725=CARTESIAN_POINT('Ctrl Pts',(-16.9156688871746,18.1268331133806,
10.5595284517789));
#198726=CARTESIAN_POINT('Ctrl Pts',(-16.9387666874942,18.088406068743,10.5621961689107));
#198727=CARTESIAN_POINT('Ctrl Pts',(-16.9588218820822,18.0569537208418,
10.5643635838444));
#198728=CARTESIAN_POINT('Ctrl Pts',(-17.0272410746549,17.9556604896947,
10.5713463289452));
#198729=CARTESIAN_POINT('Ctrl Pts',(-17.0789799731119,17.8881945334714,
10.5760031617327));
#198730=CARTESIAN_POINT('Ctrl Pts',(-17.2515555507291,17.6891936876925,
10.5903425370995));
#198731=CARTESIAN_POINT('Ctrl Pts',(-17.3850369160179,17.5697114664087,
10.599922140173));
#198732=CARTESIAN_POINT('Ctrl Pts',(-17.5506555430493,17.4554650386797,
10.6116163000165));
#198733=CARTESIAN_POINT('Ctrl Pts',(-17.5695986876368,17.4428437204718,
10.6129500225172));
#198734=CARTESIAN_POINT('Ctrl Pts',(-17.5967380789285,17.4253867345281,
10.6148571440337));
#198735=CARTESIAN_POINT('Ctrl Pts',(-17.60476948835,17.4202968258187,10.6154210712554));
#198736=CARTESIAN_POINT('Ctrl Pts',(-17.6178904033551,17.4121048139558,
10.6163417468393));
#198737=CARTESIAN_POINT('Ctrl Pts',(-17.6229592570245,17.4089697592922,
10.6166972734818));
#198738=CARTESIAN_POINT('Ctrl Pts',(-17.6336098992516,17.4024444227025,
10.6174440290005));
#198739=CARTESIAN_POINT('Ctrl Pts',(-17.6391942645076,17.3990584860299,
10.6178354123248));
#198740=CARTESIAN_POINT('Ctrl Pts',(-17.6525400345069,17.3910508407939,
10.6187704304607));
#198741=CARTESIAN_POINT('Ctrl Pts',(-17.6603154816009,17.3864528917959,
10.6193149242252));
#198742=CARTESIAN_POINT('Ctrl Pts',(-17.6867224743011,17.3710645805184,
10.6211634016877));
#198743=CARTESIAN_POINT('Ctrl Pts',(-17.7054886494271,17.360509007938,10.6224758148469));
#198744=CARTESIAN_POINT('Ctrl Pts',(-17.8832637637862,17.2640539088817,
10.6349012482034));
#198745=CARTESIAN_POINT('Ctrl Pts',(-18.052469355787,17.1985782316151,10.6467698980266));
#198746=CARTESIAN_POINT('Ctrl Pts',(-18.2356545022221,17.1534760584398,
10.6592326475943));
#198747=CARTESIAN_POINT('Ctrl Pts',(-18.2434336302385,17.1516074578773,
10.6597610031951));
#198748=CARTESIAN_POINT('Ctrl Pts',(-18.309188922122,17.1362062988076,10.6642188771182));
#198749=CARTESIAN_POINT('Ctrl Pts',(-18.3677041653715,17.1250802210653,
10.668133044275));
#198750=CARTESIAN_POINT('Ctrl Pts',(-18.4787586326482,17.1087824571137,
10.6753842595395));
#198751=CARTESIAN_POINT('Ctrl Pts',(-18.5311770082509,17.1030790832728,
10.6787333620628));
#198752=CARTESIAN_POINT('Ctrl Pts',(-18.5924273327954,17.0987212026948,
10.6825210895039));
#198753=CARTESIAN_POINT('Ctrl Pts',(-18.6011005454764,17.0981577724346,
10.6830545093525));
#198754=CARTESIAN_POINT('Ctrl Pts',(-18.6142463991786,17.097385059127,10.6838583131789));
#198755=CARTESIAN_POINT('Ctrl Pts',(-18.6187165169945,17.0971365317057,
10.6841308173092));
#198756=CARTESIAN_POINT('Ctrl Pts',(-18.6267460610666,17.0967156550779,
10.6846187926298));
#198757=CARTESIAN_POINT('Ctrl Pts',(-18.6303051474642,17.0965381117797,
10.6848345498182));
#198758=CARTESIAN_POINT('Ctrl Pts',(-18.6380446201953,17.0961716203004,
10.6853025562256));
#198759=CARTESIAN_POINT('Ctrl Pts',(-18.6422251101187,17.0959860802398,
10.6855546127155));
#198760=CARTESIAN_POINT('Ctrl Pts',(-18.6539820310099,17.0954992042487,
10.6862614724676));
#198761=CARTESIAN_POINT('Ctrl Pts',(-18.6615596585811,17.0952261715717,
10.6867147187176));
#198762=CARTESIAN_POINT('Ctrl Pts',(-18.7071304135825,17.0938293053316,
10.6894272656464));
#198763=CARTESIAN_POINT('Ctrl Pts',(-18.7451492822725,17.0936880665798,
10.6916351238748));
#198764=CARTESIAN_POINT('Ctrl Pts',(-18.8708799898052,17.0966081520467,
10.6988141803918));
#198765=CARTESIAN_POINT('Ctrl Pts',(-18.9584018316481,17.1040981807423,
10.7036165147389));
#198766=CARTESIAN_POINT('Ctrl Pts',(-19.2177353966039,17.1426405451631,
10.7178796716451));
#198767=CARTESIAN_POINT('Ctrl Pts',(-19.3864078837211,17.1894985842783,
10.7272618008282));
#198768=CARTESIAN_POINT('Ctrl Pts',(-19.5687178602881,17.2653722641146,
10.7387355062578));
#198769=CARTESIAN_POINT('Ctrl Pts',(-19.589869326526,17.2745835088188,10.7400869644461));
#198770=CARTESIAN_POINT('Ctrl Pts',(-19.6195659215021,17.2880976692996,
10.7420150709314));
#198771=CARTESIAN_POINT('Ctrl Pts',(-19.6282393648511,17.2921158637025,
10.7425819568808));
#198772=CARTESIAN_POINT('Ctrl Pts',(-19.6422842675964,17.2987384278177,
10.7435061392012));
#198773=CARTESIAN_POINT('Ctrl Pts',(-19.6476725097027,17.3013070469057,
10.7438621949091));
#198774=CARTESIAN_POINT('Ctrl Pts',(-19.6588079452328,17.3066733155458,
10.7446011689023));
#198775=CARTESIAN_POINT('Ctrl Pts',(-19.6645534694456,17.3094742715908,
10.7449841995308));
#198776=CARTESIAN_POINT('Ctrl Pts',(-19.6780797279655,17.3161443388437,
10.7458901059798));
#198777=CARTESIAN_POINT('Ctrl Pts',(-19.6858494548944,17.320035399308,10.7464137458434));
#198778=CARTESIAN_POINT('Ctrl Pts',(-19.7022696337834,17.3283854280613,
10.7475274206143));
#198779=CARTESIAN_POINT('Ctrl Pts',(-19.7109137135204,17.3328564214751,
10.7481178706126));
#198780=CARTESIAN_POINT('Ctrl Pts',(-19.7342780068654,17.3451461146347,
10.7497253096375));
#198781=CARTESIAN_POINT('Ctrl Pts',(-19.7489369729805,17.3530791920708,
10.7507463139337));
#198782=CARTESIAN_POINT('Ctrl Pts',(-19.7944990681235,17.3784364195429,
10.7539595370732));
#198783=CARTESIAN_POINT('Ctrl Pts',(-19.8250576274806,17.3964640893429,
10.7561727821335));
#198784=CARTESIAN_POINT('Ctrl Pts',(-19.9432250861952,17.4702400403586,
10.7649637045216));
#198785=CARTESIAN_POINT('Ctrl Pts',(-20.0271281137687,17.5316293211403,
10.7717300905263));
#198786=CARTESIAN_POINT('Ctrl Pts',(-20.2183047072959,17.6943561393415,
10.7882834518899));
#198787=CARTESIAN_POINT('Ctrl Pts',(-20.3201729473132,17.8012373385352,
10.7981192223337));
#198788=CARTESIAN_POINT('Ctrl Pts',(-20.4195999587139,17.9301088253,10.8082704714047));
#198789=CARTESIAN_POINT('Ctrl Pts',(-20.4289366735445,17.9424894060122,
10.8092296568668));
#198790=CARTESIAN_POINT('Ctrl Pts',(-20.4415555985968,17.9596103399693,
10.8105330107739));
#198791=CARTESIAN_POINT('Ctrl Pts',(-20.4449554683245,17.9642628221124,
10.8108848812677));
#198792=CARTESIAN_POINT('Ctrl Pts',(-20.4503344450374,17.9716870166139,
10.8114426432439));
#198793=CARTESIAN_POINT('Ctrl Pts',(-20.4523259040171,17.9744496832011,
10.8116493782275));
#198794=CARTESIAN_POINT('Ctrl Pts',(-20.4564306277032,17.9801730567957,
10.8120759591988));
#198795=CARTESIAN_POINT('Ctrl Pts',(-20.4585429301364,17.9831344073394,
10.8122957338488));
#198796=CARTESIAN_POINT('Ctrl Pts',(-20.46356691152,17.9902163356042,10.8128190985874));
#198797=CARTESIAN_POINT('Ctrl Pts',(-20.4664715352662,17.9943419390099,
10.8131222051367));
#198798=CARTESIAN_POINT('Ctrl Pts',(-20.4762589505169,18.0083496864062,
10.8141454751634));
#198799=CARTESIAN_POINT('Ctrl Pts',(-20.4830723057312,18.018280371614,10.8148610591661));
#198800=CARTESIAN_POINT('Ctrl Pts',(-20.4992636167786,18.0423168715611,
10.8165708966984));
#198801=CARTESIAN_POINT('Ctrl Pts',(-20.5085578820493,18.0564783450655,
10.8175601478));
#198802=CARTESIAN_POINT('Ctrl Pts',(-20.5429253103041,18.1102389772883,
10.8212539188106));
#198803=CARTESIAN_POINT('Ctrl Pts',(-20.5668525036089,18.1505576994599,
10.8238998568287));
#198804=CARTESIAN_POINT('Ctrl Pts',(-20.6721509071704,18.3422201706049,
10.836064728062));
#198805=CARTESIAN_POINT('Ctrl Pts',(-20.7362418679452,18.502311299053,10.8451123316752));
#198806=CARTESIAN_POINT('Ctrl Pts',(-20.79061455188,18.7073623913048,10.8569815544184));
#198807=CARTESIAN_POINT('Ctrl Pts',(-20.7998318264488,18.7466156141736,
10.8592625952486));
#198808=CARTESIAN_POINT('Ctrl Pts',(-20.8091426817149,18.7920622836997,
10.8619253734846));
#198809=CARTESIAN_POINT('Ctrl Pts',(-20.8103371897353,18.7980232051254,
10.8622750551767));
#198810=CARTESIAN_POINT('Ctrl Pts',(-20.8121465851799,18.8072589045349,
10.8628175437125));
#198811=CARTESIAN_POINT('Ctrl Pts',(-20.8127794509336,18.8105301561102,
10.863009827016));
#198812=CARTESIAN_POINT('Ctrl Pts',(-20.8188276065779,18.8421934331642,
10.8648723442165));
#198813=CARTESIAN_POINT('Ctrl Pts',(-20.8236684171136,18.8706909928592,
10.8665592676138));
#198814=CARTESIAN_POINT('Ctrl Pts',(-20.8294676985616,18.9096463622397,
10.8688832028828));
#198815=CARTESIAN_POINT('Ctrl Pts',(-20.8309342153355,18.920026150191,10.8695041441686));
#198816=CARTESIAN_POINT('Ctrl Pts',(-20.8331379327419,18.936506478661,10.8704929165883));
#198817=CARTESIAN_POINT('Ctrl Pts',(-20.8339257794662,18.9426001612473,
10.8708591438151));
#198818=CARTESIAN_POINT('Ctrl Pts',(-20.8354516394795,18.9548202125136,
10.8715948477674));
#198819=CARTESIAN_POINT('Ctrl Pts',(-20.8361894175088,18.9609465492099,
10.8719643280663));
#198820=CARTESIAN_POINT('Ctrl Pts',(-20.8376163916313,18.9732486766209,
10.8727076006313));
#198821=CARTESIAN_POINT('Ctrl Pts',(-20.8383052008012,18.9794244496828,
10.8730814012146));
#198822=CARTESIAN_POINT('Ctrl Pts',(-20.839817318438,18.9935460176408,10.8739377045565));
#198823=CARTESIAN_POINT('Ctrl Pts',(-20.8406228594342,19.0014935837608,
10.8744207624356));
#198824=CARTESIAN_POINT('Ctrl Pts',(-20.8425678109941,19.0218293107162,
10.8756597488149));
#198825=CARTESIAN_POINT('Ctrl Pts',(-20.8436430281949,19.034223173295,10.8764176797));
#198826=CARTESIAN_POINT('Ctrl Pts',(-20.8489047513554,19.1017850267102,
10.8805651162004));
#198827=CARTESIAN_POINT('Ctrl Pts',(-20.8510362031063,19.1570864420282,
10.8840180047431));
#198828=CARTESIAN_POINT('Ctrl Pts',(-20.8509995348906,19.2124033079146,
10.8875306396154));
#198829=CARTESIAN_POINT('Ctrl Pts',(-20.7225806064498,19.9371103026755,
10.9336112484111));
#198830=CARTESIAN_POINT('Ctrl Pts',(-20.7506609592852,19.8602073240716,
10.9286590708807));
#198831=CARTESIAN_POINT('Ctrl Pts',(-20.7743084251627,19.7815858993868,
10.9237068933503));
#198832=CARTESIAN_POINT('Ctrl Pts',(-20.7933361082647,19.7017380087145,
10.9187547158199));
#198833=CARTESIAN_POINT('Ctrl Pts',(-20.8123544235949,19.6219294290199,
10.9138049763619));
#198834=CARTESIAN_POINT('Ctrl Pts',(-20.826757334099,19.5408958015685,10.9088552369039));
#198835=CARTESIAN_POINT('Ctrl Pts',(-20.8364059223804,19.4591498288124,
10.9039054974458));
#198836=CARTESIAN_POINT('Ctrl Pts',(-20.8460545106619,19.3774038560563,
10.8989557579878));
#198837=CARTESIAN_POINT('Ctrl Pts',(-20.8509485990248,19.2949457663871,
10.8940060185298));
#198838=CARTESIAN_POINT('Ctrl Pts',(-20.8509995968923,19.2123064294671,
10.8890562790718));
#198839=CARTESIAN_POINT('Origin',(-18.734,19.211,0.));
#198840=CARTESIAN_POINT('',(-20.7225806064515,19.9371103026709,11.953538761502));
#198841=CARTESIAN_POINT('',(-20.72197304927,19.9368789336484,11.7337477349807));
#198842=CARTESIAN_POINT('',(-20.7225806064498,19.9371103026755,0.));
#198843=CARTESIAN_POINT('Ctrl Pts',(-20.7225806064515,19.9371103026709,
11.953538761502));
#198844=CARTESIAN_POINT('Ctrl Pts',(-20.7228709525551,19.9363151388665,
11.9534866621657));
#198845=CARTESIAN_POINT('Ctrl Pts',(-20.7231608231142,19.9355197970987,
11.9534345886039));
#198846=CARTESIAN_POINT('Ctrl Pts',(-20.7259025051468,19.9279831701196,
11.9529414976273));
#198847=CARTESIAN_POINT('Ctrl Pts',(-20.7283205545219,19.9212295301179,
11.9525023320917));
#198848=CARTESIAN_POINT('Ctrl Pts',(-20.7320650319312,19.9106012420015,
11.9518155886252));
#198849=CARTESIAN_POINT('Ctrl Pts',(-20.7334145988461,19.9067348864431,
11.9515666716498));
#198850=CARTESIAN_POINT('Ctrl Pts',(-20.7359210084883,19.8994867825828,
11.9511017653232));
#198851=CARTESIAN_POINT('Ctrl Pts',(-20.7370804930927,19.8961060592543,
11.9508856259623));
#198852=CARTESIAN_POINT('Ctrl Pts',(-20.7397139286616,19.8883638832195,
11.9503922431821));
#198853=CARTESIAN_POINT('Ctrl Pts',(-20.7411822154934,19.8840005561975,
11.950115336451));
#198854=CARTESIAN_POINT('Ctrl Pts',(-20.7456726560905,19.8705108397258,
11.9492627060604));
#198855=CARTESIAN_POINT('Ctrl Pts',(-20.7486469344233,19.8613684805354,
11.9486897318306));
#198856=CARTESIAN_POINT('Ctrl Pts',(-20.7774526028783,19.7707312530957,
11.9430544926844));
#198857=CARTESIAN_POINT('Ctrl Pts',(-20.7983905369682,19.6877524261686,
11.9382547693229));
#198858=CARTESIAN_POINT('Ctrl Pts',(-20.8385991823417,19.4747685882942,
11.9263203898874));
#198859=CARTESIAN_POINT('Ctrl Pts',(-20.8509009165884,19.3438277118629,
11.9193213392548));
#198860=CARTESIAN_POINT('Ctrl Pts',(-20.8510686215101,19.1203529362414,
11.9069620458454));
#198861=CARTESIAN_POINT('Ctrl Pts',(-20.8451100150514,19.0282216712388,
11.9017508425771));
#198862=CARTESIAN_POINT('Ctrl Pts',(-20.8313804908501,18.9231219331247,
11.8955371850017));
#198863=CARTESIAN_POINT('Ctrl Pts',(-20.8294631853462,18.9094826202811,
11.8947256882788));
#198864=CARTESIAN_POINT('Ctrl Pts',(-20.8261768233257,18.8876517413073,
11.8934182092873));
#198865=CARTESIAN_POINT('Ctrl Pts',(-20.8248923985681,18.8794476948169,
11.8929249039477));
#198866=CARTESIAN_POINT('Ctrl Pts',(-20.8225273356177,18.8649018162163,
11.8920467125576));
#198867=CARTESIAN_POINT('Ctrl Pts',(-20.8214659898609,18.8585569206174,
11.8916624432684));
#198868=CARTESIAN_POINT('Ctrl Pts',(-20.8191956392982,18.8453544986756,
11.8908603098725));
#198869=CARTESIAN_POINT('Ctrl Pts',(-20.8179816887819,18.8384979116754,
11.8904422925955));
#198870=CARTESIAN_POINT('Ctrl Pts',(-20.814744117171,18.8207228862841,11.8893548402678));
#198871=CARTESIAN_POINT('Ctrl Pts',(-20.8126683967876,18.8098142631284,
11.8886837524485));
#198872=CARTESIAN_POINT('Ctrl Pts',(-20.8033102350445,18.7626573701317,
11.8857662782635));
#198873=CARTESIAN_POINT('Ctrl Pts',(-20.7951650787619,18.7265888003379,
11.8834925177482));
#198874=CARTESIAN_POINT('Ctrl Pts',(-20.7710540793184,18.6314844222602,
11.8773804719579));
#198875=CARTESIAN_POINT('Ctrl Pts',(-20.7534685897906,18.5728987972974,
11.8734934958043));
#198876=CARTESIAN_POINT('Ctrl Pts',(-20.6816192585597,18.3664522857742,
11.8593775111725));
#198877=CARTESIAN_POINT('Ctrl Pts',(-20.6134417266214,18.2239972898535,
11.8488054516846));
#198878=CARTESIAN_POINT('Ctrl Pts',(-20.4974382960959,18.0380620774467,
11.8345700453692));
#198879=CARTESIAN_POINT('Ctrl Pts',(-20.4624924823144,17.9871481908861,
11.8306273663894));
#198880=CARTESIAN_POINT('Ctrl Pts',(-20.4198756999732,17.9305330794949,
11.8262535830398));
#198881=CARTESIAN_POINT('Ctrl Pts',(-20.4143358582464,17.9232718374406,
11.8256928370914));
#198882=CARTESIAN_POINT('Ctrl Pts',(-20.4059911951109,17.9124797763867,
11.8248600407364));
#198883=CARTESIAN_POINT('Ctrl Pts',(-20.4032218878214,17.9089218081279,
11.824585582169));
#198884=CARTESIAN_POINT('Ctrl Pts',(-20.3982421229723,17.9025658708802,
11.8240955136588));
#198885=CARTESIAN_POINT('Ctrl Pts',(-20.396035952132,17.8997646250404,11.8238796068155));
#198886=CARTESIAN_POINT('Ctrl Pts',(-20.3912401640744,17.8937068097363,
11.8234128791462));
#198887=CARTESIAN_POINT('Ctrl Pts',(-20.3886480292473,17.8904523066059,
11.8231622423955));
#198888=CARTESIAN_POINT('Ctrl Pts',(-20.3813738068635,17.8813743481205,
11.822463364273));
#198889=CARTESIAN_POINT('Ctrl Pts',(-20.3766704040939,17.8755679422125,
11.8220166239727));
#198890=CARTESIAN_POINT('Ctrl Pts',(-20.3490477271098,17.8418341753833,
11.8194219656118));
#198891=CARTESIAN_POINT('Ctrl Pts',(-20.3254458329638,17.8144704699649,
11.8173204289346));
#198892=CARTESIAN_POINT('Ctrl Pts',(-20.2470257693653,17.7281230898476,
11.8106490606755));
#198893=CARTESIAN_POINT('Ctrl Pts',(-20.1895377151286,17.6716550429534,
11.8062219757253));
#198894=CARTESIAN_POINT('Ctrl Pts',(-20.027291082339,17.5295247282931,11.794464898527));
#198895=CARTESIAN_POINT('Ctrl Pts',(-19.9173224095994,17.4504014444491,
11.7872133905136));
#198896=CARTESIAN_POINT('Ctrl Pts',(-19.7460918076039,17.3505335087033,
11.7760629959117));
#198897=CARTESIAN_POINT('Ctrl Pts',(-19.6902329598429,17.3212161992322,
11.7724493498698));
#198898=CARTESIAN_POINT('Ctrl Pts',(-19.621846323873,17.2891327117363,11.7680131915447));
#198899=CARTESIAN_POINT('Ctrl Pts',(-19.6104934895084,17.2839286153976,
11.7672764138682));
#198900=CARTESIAN_POINT('Ctrl Pts',(-19.5917883562531,17.2755537380189,
11.7660616476105));
#198901=CARTESIAN_POINT('Ctrl Pts',(-19.5844628377545,17.2723236329788,
11.7655856984044));
#198902=CARTESIAN_POINT('Ctrl Pts',(-19.571267772515,17.266594596924,11.7647279484868));
#198903=CARTESIAN_POINT('Ctrl Pts',(-19.5654048925079,17.2640804850378,
11.7643466720462));
#198904=CARTESIAN_POINT('Ctrl Pts',(-19.5529028166928,17.2587861323776,
11.763533258225));
#198905=CARTESIAN_POINT('Ctrl Pts',(-19.5462606387296,17.2560131813993,
11.7631008786842));
#198906=CARTESIAN_POINT('Ctrl Pts',(-19.5283564021436,17.2486455849479,
11.7619347168106));
#198907=CARTESIAN_POINT('Ctrl Pts',(-19.5170688000802,17.2441140885745,
11.7611988103511));
#198908=CARTESIAN_POINT('Ctrl Pts',(-19.4607286971292,17.2220577599582,
11.7575216686631));
#198909=CARTESIAN_POINT('Ctrl Pts',(-19.4151272376851,17.205983561115,11.7545322870777));
#198910=CARTESIAN_POINT('Ctrl Pts',(-19.282560368219,17.1642990972677,11.7457982305456));
#198911=CARTESIAN_POINT('Ctrl Pts',(-19.1944549551949,17.1426960662093,
11.739936186302));
#198912=CARTESIAN_POINT('Ctrl Pts',(-18.9466754574159,17.0985605996105,
11.7234139040057));
#198913=CARTESIAN_POINT('Ctrl Pts',(-18.7853973843949,17.0885030271862,
11.71258777986));
#198914=CARTESIAN_POINT('Ctrl Pts',(-18.6045520986102,17.0978666331439,
11.7012277098679));
#198915=CARTESIAN_POINT('Ctrl Pts',(-18.5845840578884,17.0991845893463,
11.6999848093547));
#198916=CARTESIAN_POINT('Ctrl Pts',(-18.5582750803121,17.1012961141556,
11.6983649188088));
#198917=CARTESIAN_POINT('Ctrl Pts',(-18.551915515977,17.10183547905,11.6979747160094));
#198918=CARTESIAN_POINT('Ctrl Pts',(-18.5416546853507,17.1027524716987,
11.6973474572141));
#198919=CARTESIAN_POINT('Ctrl Pts',(-18.5377519154395,17.1031121826482,
11.6971094161579));
#198920=CARTESIAN_POINT('Ctrl Pts',(-18.5302460191488,17.1038250138962,
11.6966526800697));
#198921=CARTESIAN_POINT('Ctrl Pts',(-18.526642796348,17.1041765387186,11.6964339010661));
#198922=CARTESIAN_POINT('Ctrl Pts',(-18.5181206678648,17.1050300189295,
11.6959175588815));
#198923=CARTESIAN_POINT('Ctrl Pts',(-18.5132025505647,17.1055399707743,
11.6956204445952));
#198924=CARTESIAN_POINT('Ctrl Pts',(-18.4968953736618,17.1072886036292,
11.6946380344148));
#198925=CARTESIAN_POINT('Ctrl Pts',(-18.4855143564462,17.1086025254199,
11.6939568356486));
#198926=CARTESIAN_POINT('Ctrl Pts',(-18.4045622378447,17.1186148809229,
11.6891396129952));
#198927=CARTESIAN_POINT('Ctrl Pts',(-18.3354431371683,17.1306732948523,
11.6851738507996));
#198928=CARTESIAN_POINT('Ctrl Pts',(-18.1364691604697,17.1756701737503,
11.6738643124207));
#198929=CARTESIAN_POINT('Ctrl Pts',(-18.0089876523703,17.217518084213,11.6667362053494));
#198930=CARTESIAN_POINT('Ctrl Pts',(-17.7930239356027,17.31189053747,11.6537590749683));
#198931=CARTESIAN_POINT('Ctrl Pts',(-17.7028124307309,17.3593247980837,
11.6480338559666));
#198932=CARTESIAN_POINT('Ctrl Pts',(-17.6044694274327,17.4204565056723,
11.6412477181595));
#198933=CARTESIAN_POINT('Ctrl Pts',(-17.5926436740793,17.4279713847902,
11.6404223877528));
#198934=CARTESIAN_POINT('Ctrl Pts',(-17.5738710901486,17.4401640303468,
11.6390968730311));
#198935=CARTESIAN_POINT('Ctrl Pts',(-17.5668757855613,17.444766667768,11.6385994860182));
#198936=CARTESIAN_POINT('Ctrl Pts',(-17.5545460456886,17.4529843878896,
11.6377165824833));
#198937=CARTESIAN_POINT('Ctrl Pts',(-17.5492004352257,17.4565825717185,
11.6373317054563));
#198938=CARTESIAN_POINT('Ctrl Pts',(-17.5381383541914,17.4641021841157,
11.6365308565426));
#198939=CARTESIAN_POINT('Ctrl Pts',(-17.532424557653,17.4680273927488,11.6361147441348));
#198940=CARTESIAN_POINT('Ctrl Pts',(-17.517724169298,17.4782327616776,11.6350377538351));
#198941=CARTESIAN_POINT('Ctrl Pts',(-17.5087669834297,17.4845547368719,
11.6343752823735));
#198942=CARTESIAN_POINT('Ctrl Pts',(-17.4708707668758,17.5117453108734,
11.6315454664862));
#198943=CARTESIAN_POINT('Ctrl Pts',(-17.4424140301682,17.5332731457457,
11.6293527447546));
#198944=CARTESIAN_POINT('Ctrl Pts',(-17.3690205726399,17.5917702736534,
11.623512295077));
#198945=CARTESIAN_POINT('Ctrl Pts',(-17.3250426906431,17.6298889701344,
11.6198210715812));
#198946=CARTESIAN_POINT('Ctrl Pts',(-17.16236303672,17.7830768316281,11.6054232915186));
#198947=CARTESIAN_POINT('Ctrl Pts',(-17.0557295954231,17.9100741052188,
11.5943090586917));
#198948=CARTESIAN_POINT('Ctrl Pts',(-16.9327538503364,18.0971605956071,
11.5797921147241));
#198949=CARTESIAN_POINT('Ctrl Pts',(-16.9025977377251,18.147471442423,11.5760536559104));
#198950=CARTESIAN_POINT('Ctrl Pts',(-16.8703032960898,18.2068072227535,
11.5718848024811));
#198951=CARTESIAN_POINT('Ctrl Pts',(-16.8660893302217,18.2146675885096,
11.5713372678744));
#198952=CARTESIAN_POINT('Ctrl Pts',(-16.8598120079354,18.2265565775295,
11.5705164760147));
#198953=CARTESIAN_POINT('Ctrl Pts',(-16.8577117519602,18.2305654571611,
11.5702409652391));
#198954=CARTESIAN_POINT('Ctrl Pts',(-16.8539791506287,18.2377460098456,
11.56974976198));
#198955=CARTESIAN_POINT('Ctrl Pts',(-16.8523419560362,18.2409150915381,
11.5695337667376));
#198956=CARTESIAN_POINT('Ctrl Pts',(-16.8488181234957,18.247778582184,11.5690676917523));
#198957=CARTESIAN_POINT('Ctrl Pts',(-16.8469343376717,18.2514743911809,
11.5688177915615));
#198958=CARTESIAN_POINT('Ctrl Pts',(-16.841713439,18.2617921425662,11.5681230434265));
#198959=CARTESIAN_POINT('Ctrl Pts',(-16.8384001992717,18.2684261913638,
11.567679667975));
#198960=CARTESIAN_POINT('Ctrl Pts',(-16.8195604469863,18.3066498680522,
11.5651433593889));
#198961=CARTESIAN_POINT('Ctrl Pts',(-16.8047878635503,18.3386074148869,
11.5630944049475));
#198962=CARTESIAN_POINT('Ctrl Pts',(-16.7602204144,18.4416960640825,11.5566645509209));
#198963=CARTESIAN_POINT('Ctrl Pts',(-16.7335097351966,18.5140961741071,
11.5524147678487));
#198964=CARTESIAN_POINT('Ctrl Pts',(-16.6547947039527,18.769640079198,11.5378226612765));
#198965=CARTESIAN_POINT('Ctrl Pts',(-16.6235566710767,18.9581825625041,
11.5276699631841));
#198966=CARTESIAN_POINT('Ctrl Pts',(-16.6172876560822,19.1699552799707,
11.5153414775381));
#198967=CARTESIAN_POINT('Ctrl Pts',(-16.6169790180816,19.1915596473639,
11.5140744879302));
#198968=CARTESIAN_POINT('Ctrl Pts',(-16.6170096727442,19.2215431645967,
11.5123018237538));
#198969=CARTESIAN_POINT('Ctrl Pts',(-16.6170679819039,19.2299217257715,
11.5118049275352));
#198970=CARTESIAN_POINT('Ctrl Pts',(-16.6172541346972,19.2443560862753,
11.5109461411231));
#198971=CARTESIAN_POINT('Ctrl Pts',(-16.6173582330624,19.2504121307511,
11.5105849976694));
#198972=CARTESIAN_POINT('Ctrl Pts',(-16.6176270766693,19.2629267712989,
11.5098369482988));
#198973=CARTESIAN_POINT('Ctrl Pts',(-16.6177954010009,19.2693852200894,
11.5094499340261));
#198974=CARTESIAN_POINT('Ctrl Pts',(-16.6182575183143,19.28446544812,11.5085439679263));
#198975=CARTESIAN_POINT('Ctrl Pts',(-16.6185744523904,19.2930863566998,
11.5080242959635));
#198976=CARTESIAN_POINT('Ctrl Pts',(-16.619766877102,19.3208912767179,11.5063424035464));
#198977=CARTESIAN_POINT('Ctrl Pts',(-16.6208506943456,19.3400649624337,
11.505173683693));
#198978=CARTESIAN_POINT('Ctrl Pts',(-16.6276561703373,19.4370273330098,
11.4992166016647));
#198979=CARTESIAN_POINT('Ctrl Pts',(-16.6374123056662,19.5144638800302,
11.4943031743117));
#198980=CARTESIAN_POINT('Ctrl Pts',(-16.6778959968728,19.7362297481452,
11.4797925704699));
#198981=CARTESIAN_POINT('Ctrl Pts',(-16.7194566174206,19.8781120566393,
11.4699322484873));
#198982=CARTESIAN_POINT('Ctrl Pts',(-16.8048782625093,20.086331582315,11.4552023150989));
#198983=CARTESIAN_POINT('Ctrl Pts',(-16.8382764015838,20.1564897065807,
11.4501988740954));
#198984=CARTESIAN_POINT('Ctrl Pts',(-16.8800160265032,20.2330191122241,
11.4448146552489));
#198985=CARTESIAN_POINT('Ctrl Pts',(-16.8846310518782,20.2413466121835,
11.4442298160458));
#198986=CARTESIAN_POINT('Ctrl Pts',(-16.8915519164469,20.2536385211883,
11.443368427247));
#198987=CARTESIAN_POINT('Ctrl Pts',(-16.893814636686,20.2576268943674,11.4430892251613));
#198988=CARTESIAN_POINT('Ctrl Pts',(-16.8978631249317,20.2647092278751,
11.4425940010038));
#198989=CARTESIAN_POINT('Ctrl Pts',(-16.8996437794134,20.2678060453785,
11.4423776556722));
#198990=CARTESIAN_POINT('Ctrl Pts',(-16.9034884891663,20.2744535606612,
11.4419136874145));
#198991=CARTESIAN_POINT('Ctrl Pts',(-16.9055550344743,20.2780027533611,
11.441666228862));
#198992=CARTESIAN_POINT('Ctrl Pts',(-16.911286643476,20.2877809677476,11.4409851225405));
#198993=CARTESIAN_POINT('Ctrl Pts',(-16.9149733362137,20.2939973372153,
11.440552854627));
#198994=CARTESIAN_POINT('Ctrl Pts',(-16.9353240135401,20.3279148239308,
11.4381976880994));
#198995=CARTESIAN_POINT('Ctrl Pts',(-16.9525899622241,20.3552519664713,
11.436311738785));
#198996=CARTESIAN_POINT('Ctrl Pts',(-17.0605740209722,20.5178501204822,
11.425102100913));
#198997=CARTESIAN_POINT('Ctrl Pts',(-17.1660346205669,20.6426802134523,
11.4164943786594));
#198998=CARTESIAN_POINT('Ctrl Pts',(-17.3700262245264,20.8342502160882,
11.4011747407821));
#198999=CARTESIAN_POINT('Ctrl Pts',(-17.4617509395734,20.9070963351511,
11.3946462198658));
#199000=CARTESIAN_POINT('Ctrl Pts',(-17.5708760650445,20.9799078817012,
11.386960603818));
#199001=CARTESIAN_POINT('Ctrl Pts',(-17.5828184775738,20.987702977319,11.3861207623949));
#199002=CARTESIAN_POINT('Ctrl Pts',(-17.6019578141564,20.9999216950296,
11.3847763512077));
#199003=CARTESIAN_POINT('Ctrl Pts',(-17.6091041613893,21.0044240130542,
11.3842747076628));
#199004=CARTESIAN_POINT('Ctrl Pts',(-17.6217595539072,21.0122917207251,
11.3833868623902));
#199005=CARTESIAN_POINT('Ctrl Pts',(-17.6272574387829,21.0156749222072,
11.3830013239591));
#199006=CARTESIAN_POINT('Ctrl Pts',(-17.6386649836771,21.0226229833315,
11.3822016777864));
#199007=CARTESIAN_POINT('Ctrl Pts',(-17.644576767613,21.0261841919482,11.3817874422534));
#199008=CARTESIAN_POINT('Ctrl Pts',(-17.6598050531408,21.0352563919834,
11.3807207806086));
#199009=CARTESIAN_POINT('Ctrl Pts',(-17.6691465147597,21.0407249016469,
11.380066818611));
#199010=CARTESIAN_POINT('Ctrl Pts',(-17.7083860721731,21.0632935443514,
11.3773209924109));
#199011=CARTESIAN_POINT('Ctrl Pts',(-17.7386559173632,21.0797335930151,
11.3752055880742));
#199012=CARTESIAN_POINT('Ctrl Pts',(-17.8186342981646,21.120676636333,11.3696201204907));
#199013=CARTESIAN_POINT('Ctrl Pts',(-17.8689251941597,21.1439780055794,
11.366111135662));
#199014=CARTESIAN_POINT('Ctrl Pts',(-18.0212889993912,21.207435511519,11.355499555825));
#199015=CARTESIAN_POINT('Ctrl Pts',(-18.1256246289486,21.2416618800848,
11.3482487140524));
#199016=CARTESIAN_POINT('Ctrl Pts',(-18.2934918689496,21.2826251689456,
11.3368351360873));
#199017=CARTESIAN_POINT('Ctrl Pts',(-18.3554938271188,21.2948454769652,
11.3326745932652));
#199018=CARTESIAN_POINT('Ctrl Pts',(-18.4215225606767,21.3048146748482,
11.3283530534595));
#199019=CARTESIAN_POINT('Ctrl Pts',(-18.4250949455776,21.3053446971034,
11.3281195818666));
#199020=CARTESIAN_POINT('Ctrl Pts',(-18.480170370975,21.3133720627818,11.3245255314925));
#199021=CARTESIAN_POINT('Ctrl Pts',(-18.531936183015,21.3189774561398,11.3212195601482));
#199022=CARTESIAN_POINT('Ctrl Pts',(-18.5925088602089,21.3232841743815,
11.3174738996854));
#199023=CARTESIAN_POINT('Ctrl Pts',(-18.6011613031151,21.3238459627956,
11.3169417738591));
#199024=CARTESIAN_POINT('Ctrl Pts',(-18.6142818875039,21.3246169417625,
11.3161395295049));
#199025=CARTESIAN_POINT('Ctrl Pts',(-18.6187475211981,21.3248651494228,
11.3158673028685));
#199026=CARTESIAN_POINT('Ctrl Pts',(-18.626772299796,21.3252856753279,11.3153796231478));
#199027=CARTESIAN_POINT('Ctrl Pts',(-18.6303311058605,21.3254631606039,
11.3151638856158));
#199028=CARTESIAN_POINT('Ctrl Pts',(-18.6380737937486,21.3258297101021,
11.3146956903862));
#199029=CARTESIAN_POINT('Ctrl Pts',(-18.642257780132,21.3260153440501,11.3144434266741));
#199030=CARTESIAN_POINT('Ctrl Pts',(-18.6540343106212,21.3265028304012,
11.3137353995251));
#199031=CARTESIAN_POINT('Ctrl Pts',(-18.6616280572531,21.3267762270104,
11.313281201361));
#199032=CARTESIAN_POINT('Ctrl Pts',(-18.707500191893,21.3281804973007,11.3105508139893));
#199033=CARTESIAN_POINT('Ctrl Pts',(-18.7458046282492,21.3283135247564,
11.3083268572928));
#199034=CARTESIAN_POINT('Ctrl Pts',(-18.872959702434,21.3253038348203,11.3010685126954));
#199035=CARTESIAN_POINT('Ctrl Pts',(-18.9616119178651,21.3176052850084,
11.2962072710144));
#199036=CARTESIAN_POINT('Ctrl Pts',(-19.2204010022461,21.2785989859009,
11.2819730642575));
#199037=CARTESIAN_POINT('Ctrl Pts',(-19.38746128238,21.2320227716173,11.2726699152892));
#199038=CARTESIAN_POINT('Ctrl Pts',(-19.5684013417516,21.1567648026964,
11.2612846863707));
#199039=CARTESIAN_POINT('Ctrl Pts',(-19.5896546695879,21.1475126621208,
11.2599269005634));
#199040=CARTESIAN_POINT('Ctrl Pts',(-19.61946836711,21.1339473449959,11.2579913033342));
#199041=CARTESIAN_POINT('Ctrl Pts',(-19.6281584055849,21.129921953056,11.2574233589185));
#199042=CARTESIAN_POINT('Ctrl Pts',(-19.6422228599753,21.1232907485736,
11.2564979211355));
#199043=CARTESIAN_POINT('Ctrl Pts',(-19.6476141498304,21.1207208839424,
11.2561416752308));
#199044=CARTESIAN_POINT('Ctrl Pts',(-19.6587502178289,21.1153547085741,
11.255402680866));
#199045=CARTESIAN_POINT('Ctrl Pts',(-19.6644933498556,21.1125551388084,
11.255019821718));
#199046=CARTESIAN_POINT('Ctrl Pts',(-19.6780039477084,21.105893347004,11.2541149944336));
#199047=CARTESIAN_POINT('Ctrl Pts',(-19.6857604778694,21.1020093175536,
11.2535922672215));
#199048=CARTESIAN_POINT('Ctrl Pts',(-19.7021492214513,21.0936763902196,
11.2524807864139));
#199049=CARTESIAN_POINT('Ctrl Pts',(-19.710775111216,21.08921555804,11.2518916208867));
#199050=CARTESIAN_POINT('Ctrl Pts',(-19.7340764993085,21.0769614403632,
11.2502886491783));
#199051=CARTESIAN_POINT('Ctrl Pts',(-19.7486911975887,21.069054587536,11.2492708561578));
#199052=CARTESIAN_POINT('Ctrl Pts',(-19.7940791437828,21.0438035813068,
11.2460704430737));
#199053=CARTESIAN_POINT('Ctrl Pts',(-19.8245111230161,21.0258614326853,
11.2438669874616));
#199054=CARTESIAN_POINT('Ctrl Pts',(-19.9426842944749,20.9521430616556,
11.2350791291115));
#199055=CARTESIAN_POINT('Ctrl Pts',(-20.0267073626804,20.8907024097566,
11.2283050634107));
#199056=CARTESIAN_POINT('Ctrl Pts',(-20.2180933636188,20.7278610628081,
11.2117366713103));
#199057=CARTESIAN_POINT('Ctrl Pts',(-20.3200485882068,20.6209137489345,
11.2018932674048));
#199058=CARTESIAN_POINT('Ctrl Pts',(-20.4195599670587,20.4919440703462,
11.1917336419008));
#199059=CARTESIAN_POINT('Ctrl Pts',(-20.4289104268596,20.47954593575,11.1907730569111));
#199060=CARTESIAN_POINT('Ctrl Pts',(-20.441544763451,20.4624044603584,11.1894681178351));
#199061=CARTESIAN_POINT('Ctrl Pts',(-20.444946669146,20.4577492689874,11.1891160379487));
#199062=CARTESIAN_POINT('Ctrl Pts',(-20.4503280637915,20.4503218225994,
11.1885580266811));
#199063=CARTESIAN_POINT('Ctrl Pts',(-20.4523199244401,20.4475586278791,
11.188351250476));
#199064=CARTESIAN_POINT('Ctrl Pts',(-20.4564248077126,20.4418350864301,
11.1879246537967));
#199065=CARTESIAN_POINT('Ctrl Pts',(-20.4585368723974,20.4388740994531,
11.1877049043681));
#199066=CARTESIAN_POINT('Ctrl Pts',(-20.4635592093266,20.4317945663319,
11.1871817122292));
#199067=CARTESIAN_POINT('Ctrl Pts',(-20.4664624389261,20.4276710034597,
11.1868787522052));
#199068=CARTESIAN_POINT('Ctrl Pts',(-20.4762402075636,20.4136773198074,
11.1858564953932));
#199069=CARTESIAN_POINT('Ctrl Pts',(-20.483045500209,20.4037587894231,11.1851417657773));
#199070=CARTESIAN_POINT('Ctrl Pts',(-20.4992145917481,20.3797567930537,
11.1834343070271));
#199071=CARTESIAN_POINT('Ctrl Pts',(-20.5084950230396,20.3656178789156,
11.1824465619013));
#199072=CARTESIAN_POINT('Ctrl Pts',(-20.542793561286,20.3119729054226,11.1787603976243));
#199073=CARTESIAN_POINT('Ctrl Pts',(-20.5666712987927,20.2717506580328,
11.17612030076));
#199074=CARTESIAN_POINT('Ctrl Pts',(-20.6411063548543,20.1363357441531,
11.1675235763867));
#199075=CARTESIAN_POINT('Ctrl Pts',(-20.6856834273888,20.0381597446355,
11.1617436503133));
#199076=CARTESIAN_POINT('Ctrl Pts',(-20.7225806899004,19.9371100741315,
11.1558808822554));
#199077=CARTESIAN_POINT('',(-20.851016007326,19.2120754280517,11.6890562438271));
#199078=CARTESIAN_POINT('Ctrl Pts',(-20.8509997268492,19.2120754163999,
11.6890562436229));
#199079=CARTESIAN_POINT('Ctrl Pts',(-20.8510361609233,19.140353500128,11.6847206650321));
#199080=CARTESIAN_POINT('Ctrl Pts',(-20.8474235543273,19.0684835617338,
11.6803850864412));
#199081=CARTESIAN_POINT('Ctrl Pts',(-20.8401430852414,18.9968731579421,
11.6760495078504));
#199082=CARTESIAN_POINT('Ctrl Pts',(-20.8328737172071,18.92537194365,11.671720540026));
#199083=CARTESIAN_POINT('Ctrl Pts',(-20.8219476405689,18.8541299663453,
11.6673915722017));
#199084=CARTESIAN_POINT('Ctrl Pts',(-20.8073980430273,18.7835546173248,
11.6630626043773));
#199085=CARTESIAN_POINT('Ctrl Pts',(-20.7928607647276,18.7130390249256,
11.658737301919));
#199086=CARTESIAN_POINT('Ctrl Pts',(-20.7747061465212,18.6431894241743,
11.6544119994608));
#199087=CARTESIAN_POINT('Ctrl Pts',(-20.7530189912436,18.5744064774147,
11.6500866970025));
#199088=CARTESIAN_POINT('Ctrl Pts',(-20.7313426460971,18.5056578160493,
11.6457635505248));
#199089=CARTESIAN_POINT('Ctrl Pts',(-20.7061374043778,18.4379752252391,
11.6414404040472));
#199090=CARTESIAN_POINT('Ctrl Pts',(-20.6775383611331,18.3717457841607,
11.6371172575695));
#199091=CARTESIAN_POINT('Ctrl Pts',(-20.6489436148164,18.3055262938746,
11.6327947606328));
#199092=CARTESIAN_POINT('Ctrl Pts',(-20.6169562761199,18.2407599735633,
11.6284722636961));
#199093=CARTESIAN_POINT('Ctrl Pts',(-20.5817594783855,18.1778137099067,
11.6241497667594));
#199094=CARTESIAN_POINT('Ctrl Pts',(-20.5465310340247,18.1148108491444,
11.6198233833201));
#199095=CARTESIAN_POINT('Ctrl Pts',(-20.5080876068594,18.0536317475177,
11.6154969998808));
#199096=CARTESIAN_POINT('Ctrl Pts',(-20.4666577218297,17.9946175687786,
11.6111706164415));
#199097=CARTESIAN_POINT('Ctrl Pts',(-20.4252103606638,17.9355784964193,
11.6068424080281));
#199098=CARTESIAN_POINT('Ctrl Pts',(-20.3807743381433,17.878706555747,11.6025141996147));
#199099=CARTESIAN_POINT('Ctrl Pts',(-20.3336191165842,17.8243105315686,
11.5981859912013));
#199100=CARTESIAN_POINT('Ctrl Pts',(-20.2863774057356,17.7698147374533,
11.5938498442467));
#199101=CARTESIAN_POINT('Ctrl Pts',(-20.2364068761987,17.7178042891277,
11.5895136972921));
#199102=CARTESIAN_POINT('Ctrl Pts',(-20.184014156115,17.6685513146085,11.5851775503375));
#199103=CARTESIAN_POINT('Ctrl Pts',(-20.1349615139514,17.6224382567118,
11.5811178362285));
#199104=CARTESIAN_POINT('Ctrl Pts',(-20.0837862726332,17.578742122906,11.5770581221195));
#199105=CARTESIAN_POINT('Ctrl Pts',(-20.0307638001155,17.5376522636612,
11.5729984080105));
#199106=CARTESIAN_POINT('Ctrl Pts',(-19.9734509743369,17.4932375875374,
11.5686101990796));
#199107=CARTESIAN_POINT('Ctrl Pts',(-19.9137418045022,17.4516841015565,
11.5642219901487));
#199108=CARTESIAN_POINT('Ctrl Pts',(-19.8519537768687,17.4132602099344,
11.5598337812178));
#199109=CARTESIAN_POINT('Ctrl Pts',(-19.7902574529129,17.3748933457383,
11.5554520851166));
#199110=CARTESIAN_POINT('Ctrl Pts',(-19.7264888022835,17.3396471078962,
11.5510703890153));
#199111=CARTESIAN_POINT('Ctrl Pts',(-19.6609970987603,17.3077487346937,
11.546688692914));
#199112=CARTESIAN_POINT('Ctrl Pts',(-19.5955823532007,17.2758878446183,
11.5423121456544));
#199113=CARTESIAN_POINT('Ctrl Pts',(-19.5284490083959,17.2473672144277,
11.5379355983948));
#199114=CARTESIAN_POINT('Ctrl Pts',(-19.45997246989,17.2223690707017,11.5335590511351));
#199115=CARTESIAN_POINT('Ctrl Pts',(-19.3915393582096,17.1973867804351,
11.5291852794182));
#199116=CARTESIAN_POINT('Ctrl Pts',(-19.32176519499,17.1759227092788,11.5248115077012));
#199117=CARTESIAN_POINT('Ctrl Pts',(-19.2510456730813,17.1581111155379,
11.5204377359842));
#199118=CARTESIAN_POINT('Ctrl Pts',(-19.1803476713606,17.1403049419248,
11.5160652952207));
#199119=CARTESIAN_POINT('Ctrl Pts',(-19.1087053495643,17.1261491568768,
11.5116928544571));
#199120=CARTESIAN_POINT('Ctrl Pts',(-19.0365282611614,17.1157277858954,
11.5073204136936));
#199121=CARTESIAN_POINT('Ctrl Pts',(-18.9643493271828,17.1053061484385,
11.5029478611262));
#199122=CARTESIAN_POINT('Ctrl Pts',(-18.8916360771615,17.0986191815879,
11.4985753085589));
#199123=CARTESIAN_POINT('Ctrl Pts',(-18.8188052520572,17.0956992957918,
11.4942027559916));
#199124=CARTESIAN_POINT('Ctrl Pts',(-18.7458988403753,17.0927763796282,
11.4898256654243));
#199125=CARTESIAN_POINT('Ctrl Pts',(-18.6728750930031,17.0936283697016,
11.4854485748569));
#199126=CARTESIAN_POINT('Ctrl Pts',(-18.6001519939629,17.0982355286781,
11.4810714842896));
#199127=CARTESIAN_POINT('Ctrl Pts',(-18.5273891781392,17.1028452037952,
11.4766920032307));
#199128=CARTESIAN_POINT('Ctrl Pts',(-18.4549278170831,17.1112140756296,
11.4723125221717));
#199129=CARTESIAN_POINT('Ctrl Pts',(-18.3831792948545,17.1232706514394,
11.4679330411128));
#199130=CARTESIAN_POINT('Ctrl Pts',(-18.3113035988519,17.135348597449,11.4635457974531));
#199131=CARTESIAN_POINT('Ctrl Pts',(-18.2401437361935,17.1511271959047,
11.4591585537934));
#199132=CARTESIAN_POINT('Ctrl Pts',(-18.1700988737773,17.1704842515078,
11.4547713101336));
#199133=CARTESIAN_POINT('Ctrl Pts',(-18.1224751168407,17.1836451840766,
11.4517884071988));
#199134=CARTESIAN_POINT('Ctrl Pts',(-18.0753664841793,17.1984592758342,
11.448805504264));
#199135=CARTESIAN_POINT('Ctrl Pts',(-18.0288930166915,17.2148754692932,
11.4458226013291));
#199136=CARTESIAN_POINT('Ctrl Pts',(-17.960524957276,17.2390256640268,11.4414343923982));
#199137=CARTESIAN_POINT('Ctrl Pts',(-17.8932656103902,17.2667395128395,
11.4370461834673));
#199138=CARTESIAN_POINT('Ctrl Pts',(-17.8275125107934,17.2978953421436,
11.4326579745364));
#199139=CARTESIAN_POINT('Ctrl Pts',(-17.7618569996983,17.3290049310313,
11.4282762784352));
#199140=CARTESIAN_POINT('Ctrl Pts',(-17.6977037303935,17.3635461545568,
11.4238945823339));
#199141=CARTESIAN_POINT('Ctrl Pts',(-17.6354328295884,17.401348328519,11.4195128862326));
#199142=CARTESIAN_POINT('Ctrl Pts',(-17.5732351020475,17.4391060819184,
11.415136338973));
#199143=CARTESIAN_POINT('Ctrl Pts',(-17.5129157592866,17.4801169246316,
11.4107597917133));
#199144=CARTESIAN_POINT('Ctrl Pts',(-17.454831224922,17.5241638357963,11.4063832444537));
#199145=CARTESIAN_POINT('Ctrl Pts',(-17.3967835269249,17.5681828130501,
11.4020094727367));
#199146=CARTESIAN_POINT('Ctrl Pts',(-17.3409682086663,17.6152337476986,
11.3976357010197));
#199147=CARTESIAN_POINT('Ctrl Pts',(-17.2877123411686,17.6650565961484,
11.3932619293028));
#199148=CARTESIAN_POINT('Ctrl Pts',(-17.2344726796103,17.7148642833382,
11.3888894885392));
#199149=CARTESIAN_POINT('Ctrl Pts',(-17.1837912746023,17.7674418803649,
11.3845170477757));
#199150=CARTESIAN_POINT('Ctrl Pts',(-17.135960461819,17.8224904989845,11.3801446070121));
#199151=CARTESIAN_POINT('Ctrl Pts',(-17.0881284259965,17.8775405252034,
11.3757720544447));
#199152=CARTESIAN_POINT('Ctrl Pts',(-17.0431474419897,17.9350613330224,
11.3713995018774));
#199153=CARTESIAN_POINT('Ctrl Pts',(-17.001270335834,17.994720052406,11.36702694931));
#199154=CARTESIAN_POINT('Ctrl Pts',(-16.959349768038,18.0544406878589,11.3626498587427));
#199155=CARTESIAN_POINT('Ctrl Pts',(-16.9205397874117,18.1163032692078,
11.3582727681754));
#199156=CARTESIAN_POINT('Ctrl Pts',(-16.8850500448045,18.179945654593,11.3538956776081));
#199157=CARTESIAN_POINT('Ctrl Pts',(-16.8495409199317,18.2436227974469,
11.3495161965491));
#199158=CARTESIAN_POINT('Ctrl Pts',(-16.8173558563405,18.3090812464319,
11.3451367154902));
#199159=CARTESIAN_POINT('Ctrl Pts',(-16.7886574143382,18.3759363949911,
11.3407572344312));
#199160=CARTESIAN_POINT('Ctrl Pts',(-16.75990810454,18.4429100438524,11.3363699907715));
#199161=CARTESIAN_POINT('Ctrl Pts',(-16.7346579248205,18.511284883135,11.3319827471118));
#199162=CARTESIAN_POINT('Ctrl Pts',(-16.7130201897423,18.5806591346496,
11.3275955034521));
#199163=CARTESIAN_POINT('Ctrl Pts',(-16.6983086148963,18.6278269407927,
11.3246126005173));
#199164=CARTESIAN_POINT('Ctrl Pts',(-16.68526591231,18.6754564326548,11.3216296975824));
#199165=CARTESIAN_POINT('Ctrl Pts',(-16.6739141265779,18.7234190383877,
11.3186467946476));
#199166=CARTESIAN_POINT('Ctrl Pts',(-16.6572142846389,18.7939777992408,
11.3142585857167));
#199167=CARTESIAN_POINT('Ctrl Pts',(-16.6441110368838,18.8655332466771,
11.3098703767858));
#199168=CARTESIAN_POINT('Ctrl Pts',(-16.6347172531061,18.9376852572698,
11.3054821678549));
#199169=CARTESIAN_POINT('Ctrl Pts',(-16.6253374112611,19.0097301823155,
11.3011004717537));
#199170=CARTESIAN_POINT('Ctrl Pts',(-16.6196561660671,19.0823694384939,
11.2967187756524));
#199171=CARTESIAN_POINT('Ctrl Pts',(-16.6177357545009,19.1551910112778,
11.2923370795512));
#199172=CARTESIAN_POINT('Ctrl Pts',(-16.6158175995711,19.2279270129186,
11.2879605322915));
#199173=CARTESIAN_POINT('Ctrl Pts',(-16.6176515119966,19.3008444257661,
11.2835839850319));
#199174=CARTESIAN_POINT('Ctrl Pts',(-16.6232479369201,19.3735260846875,
11.2792074377722));
#199175=CARTESIAN_POINT('Ctrl Pts',(-16.6288408126722,19.4461616499572,
11.2748336660553));
#199176=CARTESIAN_POINT('Ctrl Pts',(-16.6381914295875,19.5185612781807,
11.2704598943383));
#199177=CARTESIAN_POINT('Ctrl Pts',(-16.6512581694981,19.5903091977233,
11.2660861226213));
#199178=CARTESIAN_POINT('Ctrl Pts',(-16.6643209331558,19.6620352841331,
11.2617136818578));
#199179=CARTESIAN_POINT('Ctrl Pts',(-16.6810974883882,19.7331095812962,
11.2573412410942));
#199180=CARTESIAN_POINT('Ctrl Pts',(-16.701494753238,19.803124498636,11.2529688003307));
#199181=CARTESIAN_POINT('Ctrl Pts',(-16.7218925396482,19.873141206265,11.2485962477633));
#199182=CARTESIAN_POINT('Ctrl Pts',(-16.7459110826477,19.9420980177238,
11.244223695196));
#199183=CARTESIAN_POINT('Ctrl Pts',(-16.7734073411525,20.0096021700904,
11.2398511426286));
#199184=CARTESIAN_POINT('Ctrl Pts',(-16.8009321363113,20.0771763808124,
11.2354740520613));
#199185=CARTESIAN_POINT('Ctrl Pts',(-16.8319416708365,20.143294474674,11.231096961494));
#199186=CARTESIAN_POINT('Ctrl Pts',(-16.8662449207626,20.2075841479689,
11.2267198709266));
#199187=CARTESIAN_POINT('Ctrl Pts',(-16.9005669049666,20.2719089322405,
11.2223403898677));
#199188=CARTESIAN_POINT('Ctrl Pts',(-16.938185937055,20.3344028942419,11.2179609088088));
#199189=CARTESIAN_POINT('Ctrl Pts',(-16.9788666145899,20.394721166246,11.2135814277498));
#199190=CARTESIAN_POINT('Ctrl Pts',(-17.0196193983526,20.4551463519822,
11.2091941840901));
#199191=CARTESIAN_POINT('Ctrl Pts',(-17.0634443742617,20.5133877608711,
11.2048069404304));
#199192=CARTESIAN_POINT('Ctrl Pts',(-17.1100650454665,20.5691326383841,
11.2004196967707));
#199193=CARTESIAN_POINT('Ctrl Pts',(-17.1417626095285,20.6070337835293,
11.1974367938359));
#199194=CARTESIAN_POINT('Ctrl Pts',(-17.1747517071183,20.643781572932,11.194453890901));
#199195=CARTESIAN_POINT('Ctrl Pts',(-17.2089361619795,20.6792878770739,
11.1914709879662));
#199196=CARTESIAN_POINT('Ctrl Pts',(-17.259225605987,20.7315219203344,11.1870827790353));
#199197=CARTESIAN_POINT('Ctrl Pts',(-17.3122998738988,20.7812712846034,
11.1826945701044));
#199198=CARTESIAN_POINT('Ctrl Pts',(-17.3678836195123,20.8282244850246,
11.1783063611735));
#199199=CARTESIAN_POINT('Ctrl Pts',(-17.4233848696314,20.8751079991114,
11.1739246650723));
#199200=CARTESIAN_POINT('Ctrl Pts',(-17.4813878383958,20.9192032789,11.169542968971));
#199201=CARTESIAN_POINT('Ctrl Pts',(-17.5415797744862,20.9602349772931,
11.1651612728698));
#199202=CARTESIAN_POINT('Ctrl Pts',(-17.6017009802615,21.0012184601752,
11.1607847256101));
#199203=CARTESIAN_POINT('Ctrl Pts',(-17.6640056470485,21.0391452426346,
11.1564081783505));
#199204=CARTESIAN_POINT('Ctrl Pts',(-17.7281486587461,21.0737807383849,
11.1520316310908));
#199205=CARTESIAN_POINT('Ctrl Pts',(-17.7922509918778,21.1083942688071,
11.1476578593739));
#199206=CARTESIAN_POINT('Ctrl Pts',(-17.8581889333121,21.1397204253384,
11.1432840876569));
#199207=CARTESIAN_POINT('Ctrl Pts',(-17.9255903577763,21.1675691529715,
11.1389103159399));
#199208=CARTESIAN_POINT('Ctrl Pts',(-17.9929712717607,21.1954094061433,
11.1345378751764));
#199209=CARTESIAN_POINT('Ctrl Pts',(-18.0618143390783,21.2197741471641,
11.1301654344128));
#199210=CARTESIAN_POINT('Ctrl Pts',(-18.1317264570587,21.2405210221806,
11.1257929936492));
#199211=CARTESIAN_POINT('Ctrl Pts',(-18.2016403626996,21.261268427697,11.1214204410819));
#199212=CARTESIAN_POINT('Ctrl Pts',(-18.2726229102623,21.2783976482244,
11.1170478885146));
#199213=CARTESIAN_POINT('Ctrl Pts',(-18.3442664228596,21.2918163635577,
11.1126753359472));
#199214=CARTESIAN_POINT('Ctrl Pts',(-18.4159842897966,21.3052490053399,
11.1082982453799));
#199215=CARTESIAN_POINT('Ctrl Pts',(-18.4883640162152,21.3149633643478,
11.1039211548125));
#199216=CARTESIAN_POINT('Ctrl Pts',(-18.5609891559671,21.3209185405714,
11.0995440642452));
#199217=CARTESIAN_POINT('Ctrl Pts',(-18.6336539590034,21.3268769691377,
11.0951645831863));
#199218=CARTESIAN_POINT('Ctrl Pts',(-18.7065639597306,21.329072112832,11.0907851021273));
#199219=CARTESIAN_POINT('Ctrl Pts',(-18.779301760092,21.3275152374912,11.0864056210684));
#199220=CARTESIAN_POINT('Ctrl Pts',(-18.8521684877163,21.3259556025994,
11.0820183774087));
#199221=CARTESIAN_POINT('Ctrl Pts',(-18.9248619239423,21.3206307033084,
11.077631133749));
#199222=CARTESIAN_POINT('Ctrl Pts',(-18.9969694292048,21.311603741619,11.0732438900892));
#199223=CARTESIAN_POINT('Ctrl Pts',(-19.0459955845206,21.3054662775061,
11.0702609871544));
#199224=CARTESIAN_POINT('Ctrl Pts',(-19.0947510327821,21.2976185484977,
11.0672780842196));
#199225=CARTESIAN_POINT('Ctrl Pts',(-19.1431096126279,21.2880937207684,
11.0642951812848));
#199226=CARTESIAN_POINT('Ctrl Pts',(-19.21425089902,21.2740815537551,11.0599069723539));
#199227=CARTESIAN_POINT('Ctrl Pts',(-19.2848103359501,21.2563828809337,
11.055518763423));
#199228=CARTESIAN_POINT('Ctrl Pts',(-19.3543769742709,21.2350606240413,
11.0511305544921));
#199229=CARTESIAN_POINT('Ctrl Pts',(-19.4238403641662,21.2137700129134,
11.0467488583908));
#199230=CARTESIAN_POINT('Ctrl Pts',(-19.4923134231182,21.1888666339676,
11.0423671622895));
#199231=CARTESIAN_POINT('Ctrl Pts',(-19.5593953414354,21.1604644214083,
11.0379854661882));
#199232=CARTESIAN_POINT('Ctrl Pts',(-19.6263984331598,21.1320955837092,
11.0336089189286));
#199233=CARTESIAN_POINT('Ctrl Pts',(-19.6920131895949,21.1002362668755,
11.029232371669));
#199234=CARTESIAN_POINT('Ctrl Pts',(-19.7558555559983,21.065049681825,11.0248558244093));
#199235=CARTESIAN_POINT('Ctrl Pts',(-19.8196574345007,21.0298854115954,
11.0204820526924));
#199236=CARTESIAN_POINT('Ctrl Pts',(-19.881688731758,20.9913982921376,11.0161082809754));
#199237=CARTESIAN_POINT('Ctrl Pts',(-19.9415882172339,20.9497983487448,
11.0117345092584));
#199238=CARTESIAN_POINT('Ctrl Pts',(-20.0014694750955,20.9082110643544,
11.0073620684949));
#199239=CARTESIAN_POINT('Ctrl Pts',(-20.059219813117,20.8635131115926,11.0029896277313));
#199240=CARTESIAN_POINT('Ctrl Pts',(-20.1145067552164,20.8159579741544,
10.9986171869677));
#199241=CARTESIAN_POINT('Ctrl Pts',(-20.1697951110089,20.7684016207262,
10.9942446344004));
#199242=CARTESIAN_POINT('Ctrl Pts',(-20.2226195814197,20.7179882536478,
10.989872081833));
#199243=CARTESIAN_POINT('Ctrl Pts',(-20.2726818719995,20.665010693489,10.9854995292657));
#199244=CARTESIAN_POINT('Ctrl Pts',(-20.3227961191127,20.61197815122,10.9811224386984));
#199245=CARTESIAN_POINT('Ctrl Pts',(-20.370142130828,20.5563764539256,10.976745348131));
#199246=CARTESIAN_POINT('Ctrl Pts',(-20.4144601023079,20.4985336285127,
10.9723682575637));
#199247=CARTESIAN_POINT('Ctrl Pts',(-20.4588022774771,20.4406592129859,
10.9679887765048));
#199248=CARTESIAN_POINT('Ctrl Pts',(-20.5001128464811,20.3805416302794,
10.9636092954458));
#199249=CARTESIAN_POINT('Ctrl Pts',(-20.5381753524546,20.3185379440883,
10.9592298143869));
#199250=CARTESIAN_POINT('Ctrl Pts',(-20.5763053239643,20.2564243567798,
10.9548425707271));
#199251=CARTESIAN_POINT('Ctrl Pts',(-20.6111755046332,20.192418413908,10.9504553270674));
#199252=CARTESIAN_POINT('Ctrl Pts',(-20.6426156833716,20.1269012900897,
10.9460680834077));
#199253=CARTESIAN_POINT('Ctrl Pts',(-20.6639919753451,20.0823559591087,
10.9430851804729));
#199254=CARTESIAN_POINT('Ctrl Pts',(-20.6837836766027,20.0371125159695,
10.9401022775381));
#199255=CARTESIAN_POINT('Ctrl Pts',(-20.7019503858965,19.9912949946334,
10.9371193746033));
#199256=CARTESIAN_POINT('Ctrl Pts',(-20.7090722076132,19.9733333366809,
10.9359499992059));
#199257=CARTESIAN_POINT('Ctrl Pts',(-20.7159498922732,19.955269678145,10.9347806238085));
#199258=CARTESIAN_POINT('Ctrl Pts',(-20.7225806064498,19.9371103026755,
10.9336112484111));
#199259=CARTESIAN_POINT('Ctrl Pts',(-20.7219730492699,19.9368789336487,
11.7337477349808));
#199260=CARTESIAN_POINT('Ctrl Pts',(-20.7875398502892,19.7626326972607,
11.7225565615512));
#199261=CARTESIAN_POINT('Ctrl Pts',(-20.8444161920097,19.5201105099742,
11.7076594095651));
#199262=CARTESIAN_POINT('Ctrl Pts',(-20.8542040955766,19.273466074897,11.692762257579));
#199263=CARTESIAN_POINT('Ctrl Pts',(-20.853822991173,19.2120774369757,11.6890562790225));
#199264=CARTESIAN_POINT('Origin',(-18.734,19.211,0.));
#199265=CARTESIAN_POINT('',(-20.7225806071911,19.9371103006456,12.75653014821));
#199266=CARTESIAN_POINT('',(-20.7225806018034,19.9371103154006,12.5316746994897));
#199267=CARTESIAN_POINT('',(-20.7225806064498,19.9371103026755,0.));
#199268=CARTESIAN_POINT('',(-20.850999901999,19.2116441554391,12.7090270029862));
#199269=CARTESIAN_POINT('Ctrl Pts',(-20.7225806071911,19.9371103006456,
12.75653014821));
#199270=CARTESIAN_POINT('Ctrl Pts',(-20.7242579214128,19.9325166810117,
12.7562119943992));
#199271=CARTESIAN_POINT('Ctrl Pts',(-20.725919378386,19.927917086162,12.7558935117464));
#199272=CARTESIAN_POINT('Ctrl Pts',(-20.7864431000032,19.7585277763737,
12.7441682245227));
#199273=CARTESIAN_POINT('Ctrl Pts',(-20.8246620318631,19.5870863820778,
12.7323482183352));
#199274=CARTESIAN_POINT('Ctrl Pts',(-20.8438467742753,19.3868429567836,
12.7196400581752));
#199275=CARTESIAN_POINT('Ctrl Pts',(-20.8458598061736,19.3607413110147,
12.7180060566353));
#199276=CARTESIAN_POINT('Ctrl Pts',(-20.8477953021789,19.3276490835098,
12.715968468761));
#199277=CARTESIAN_POINT('Ctrl Pts',(-20.8481679338033,19.320688372186,12.7155417813462));
#199278=CARTESIAN_POINT('Ctrl Pts',(-20.8487046765667,19.3096400718763,
12.7148676844595));
#199279=CARTESIAN_POINT('Ctrl Pts',(-20.8488913284795,19.3055537003482,
12.7146190451098));
#199280=CARTESIAN_POINT('Ctrl Pts',(-20.8492163340247,19.2979552396666,
12.7141580150344));
#199281=CARTESIAN_POINT('Ctrl Pts',(-20.8493577841497,19.2944433860608,
12.7139454585469));
#199282=CARTESIAN_POINT('Ctrl Pts',(-20.8496218268413,19.2874551214259,
12.713523515112));
#199283=CARTESIAN_POINT('Ctrl Pts',(-20.849744596623,19.2839787781355,12.7133141197207));
#199284=CARTESIAN_POINT('Ctrl Pts',(-20.850006252835,19.2760131563302,12.7128354340013));
#199285=CARTESIAN_POINT('Ctrl Pts',(-20.8501394227246,19.2715236891833,
12.7125664580095));
#199286=CARTESIAN_POINT('Ctrl Pts',(-20.8504746952252,19.2588612713493,
12.711810028741));
#199287=CARTESIAN_POINT('Ctrl Pts',(-20.8506437465308,19.2506874266378,
12.7113243345654));
#199288=CARTESIAN_POINT('Ctrl Pts',(-20.8509186141132,19.2322240492644,
12.7102326836416));
#199289=CARTESIAN_POINT('Ctrl Pts',(-20.8509967709478,19.2219342726963,
12.7096281222256));
#199290=CARTESIAN_POINT('Ctrl Pts',(-20.850999901999,19.2116441554391,12.7090270029862));
#199291=CARTESIAN_POINT('Ctrl Pts',(-20.8509999014158,19.2116460691223,
12.7090271147781));
#199292=CARTESIAN_POINT('Ctrl Pts',(-20.8510612404263,19.0106541402446,
12.6972857323756));
#199293=CARTESIAN_POINT('Ctrl Pts',(-20.8224997951858,18.810633809048,12.6868413446637));
#199294=CARTESIAN_POINT('Ctrl Pts',(-20.7414593028743,18.533101317908,12.6708787977931));
#199295=CARTESIAN_POINT('Ctrl Pts',(-20.7115380387582,18.4502239235883,
12.6659224450404));
#199296=CARTESIAN_POINT('Ctrl Pts',(-20.6684004803174,18.3506490097334,
12.6595976067165));
#199297=CARTESIAN_POINT('Ctrl Pts',(-20.6599809133746,18.3319627297392,
12.6583942611593));
#199298=CARTESIAN_POINT('Ctrl Pts',(-20.6475366195967,18.3053814065272,
12.6566576095812));
#199299=CARTESIAN_POINT('Ctrl Pts',(-20.643731405833,18.2973844433655,12.6561318752003));
#199300=CARTESIAN_POINT('Ctrl Pts',(-20.6370469607357,18.2835607822067,
12.6552173071385));
#199301=CARTESIAN_POINT('Ctrl Pts',(-20.6341908486712,18.277722991476,12.6548292816806));
#199302=CARTESIAN_POINT('Ctrl Pts',(-20.6286469714142,18.2665224533086,
12.6540812987143));
#199303=CARTESIAN_POINT('Ctrl Pts',(-20.6259632017933,18.2611577897345,
12.6537214839144));
#199304=CARTESIAN_POINT('Ctrl Pts',(-20.6188714145975,18.2471311235001,
12.6527765706384));
#199305=CARTESIAN_POINT('Ctrl Pts',(-20.614426520458,18.238488017101,12.6521901792748));
#199306=CARTESIAN_POINT('Ctrl Pts',(-20.5987859039375,18.2085829492576,
12.6501466443006));
#199307=CARTESIAN_POINT('Ctrl Pts',(-20.5872881357366,18.1874818406939,
12.6486788520719));
#199308=CARTESIAN_POINT('Ctrl Pts',(-20.503482796716,18.0397230352569,12.6382123895947));
#199309=CARTESIAN_POINT('Ctrl Pts',(-20.4186277887561,17.9206611186917,
12.6287469226873));
#199310=CARTESIAN_POINT('Ctrl Pts',(-20.2316748408658,17.7085295413942,
12.6100860236023));
#199311=CARTESIAN_POINT('Ctrl Pts',(-20.1313546897213,17.6148004864574,
12.6009623563512));
#199312=CARTESIAN_POINT('Ctrl Pts',(-20.0125946991022,17.5236808059512,
12.5915883312335));
#199313=CARTESIAN_POINT('Ctrl Pts',(-20.0024435423399,17.5160364416838,
12.590797638063));
#199314=CARTESIAN_POINT('Ctrl Pts',(-19.9868049689495,17.5044789444255,
12.5895963507252));
#199315=CARTESIAN_POINT('Ctrl Pts',(-19.9813668578717,17.5004999772129,
12.5891816906442));
#199316=CARTESIAN_POINT('Ctrl Pts',(-19.9723753383292,17.4939867302626,
12.5885012513126));
#199317=CARTESIAN_POINT('Ctrl Pts',(-19.9688329714792,17.4914373869045,
12.5882344921829));
#199318=CARTESIAN_POINT('Ctrl Pts',(-19.9619704832989,17.4865307856064,
12.5877202811318));
#199319=CARTESIAN_POINT('Ctrl Pts',(-19.9586513981957,17.4841721183665,
12.5874727348678));
#199320=CARTESIAN_POINT('Ctrl Pts',(-19.9553158056823,17.4818161743379,
12.5872251308145));
#199321=CARTESIAN_POINT('Ctrl Pts',(-19.9553061150038,17.4818093298901,
12.5872244114766));
#199322=CARTESIAN_POINT('Ctrl Pts',(-19.9552866993953,17.4817956170476,
12.5872229702781));
#199323=CARTESIAN_POINT('Ctrl Pts',(-19.9552769742806,17.4817887485233,
12.5872222484039));
#199324=CARTESIAN_POINT('Ctrl Pts',(-19.9552574896208,17.481774987404,12.5872208021199));
#199325=CARTESIAN_POINT('Ctrl Pts',(-19.9552477298694,17.4817680946641,
12.5872200776947));
#199326=CARTESIAN_POINT('Ctrl Pts',(-19.9552275533345,17.4817538454172,
12.5872185800965));
#199327=CARTESIAN_POINT('Ctrl Pts',(-19.9552171369376,17.4817464892004,
12.5872178069536));
#199328=CARTESIAN_POINT('Ctrl Pts',(-19.9551961361628,17.4817316584205,
12.5872162482226));
#199329=CARTESIAN_POINT('Ctrl Pts',(-19.9551855518082,17.4817241838784,
12.5872154626366));
#199330=CARTESIAN_POINT('Ctrl Pts',(-19.9551642116505,17.4817091140131,
12.5872138787634));
#199331=CARTESIAN_POINT('Ctrl Pts',(-19.9551534559073,17.4817015187369,
12.587213080481));
#199332=CARTESIAN_POINT('Ctrl Pts',(-19.955131769556,17.481686205005,12.5872114709625));
#199333=CARTESIAN_POINT('Ctrl Pts',(-19.9551208386152,17.4816784863193,
12.5872106597021));
#199334=CARTESIAN_POINT('Ctrl Pts',(-19.9550987979607,17.481662923024,12.5872090239387));
#199335=CARTESIAN_POINT('Ctrl Pts',(-19.9550876883188,17.4816550784701,
12.5872081994415));
#199336=CARTESIAN_POINT('Ctrl Pts',(-19.9550652861652,17.4816392605609,
12.5872065369018));
#199337=CARTESIAN_POINT('Ctrl Pts',(-19.9550539938539,17.4816312873523,
12.5872056988745));
#199338=CARTESIAN_POINT('Ctrl Pts',(-19.955031222665,17.4816152095399,12.5872040090017));
#199339=CARTESIAN_POINT('Ctrl Pts',(-19.9550197434877,17.4816071047299,
12.5872031571343));
#199340=CARTESIAN_POINT('Ctrl Pts',(-19.9549965942264,17.4815907606666,
12.5872014392605));
#199341=CARTESIAN_POINT('Ctrl Pts',(-19.9549849244509,17.4815825216369,
12.5872005732774));
#199342=CARTESIAN_POINT('Ctrl Pts',(-19.9549613899256,17.4815659062798,
12.5871988268716));
#199343=CARTESIAN_POINT('Ctrl Pts',(-19.9549495249503,17.4815575297991,
12.5871979464327));
#199344=CARTESIAN_POINT('Ctrl Pts',(-19.9549255955538,17.4815406364012,
12.587196170785));
#199345=CARTESIAN_POINT('Ctrl Pts',(-19.9549135313658,17.4815321196547,
12.5871952755941));
#199346=CARTESIAN_POINT('Ctrl Pts',(-19.9548891993164,17.4815149427595,
12.5871934701301));
#199347=CARTESIAN_POINT('Ctrl Pts',(-19.9548769310923,17.4815062823612,
12.5871925598306));
#199348=CARTESIAN_POINT('Ctrl Pts',(-19.9548521861696,17.4814888147924,
12.5871907237951));
#199349=CARTESIAN_POINT('Ctrl Pts',(-19.9548397097018,17.4814800077916,
12.5871897980766));
#199350=CARTESIAN_POINT('Ctrl Pts',(-19.9519913099692,17.4794694000664,
12.5869784586612));
#199351=CARTESIAN_POINT('Ctrl Pts',(-19.9491505071673,17.4774746050912,
12.5867685355329));
#199352=CARTESIAN_POINT('Ctrl Pts',(-19.94255546995,17.4728677863359,12.5862831463832));
#199353=CARTESIAN_POINT('Ctrl Pts',(-19.9387976744691,17.4702609383892,
12.5860080348999));
#199354=CARTESIAN_POINT('Ctrl Pts',(-19.9272418710299,17.4622998218784,
12.5851663937687));
#199355=CARTESIAN_POINT('Ctrl Pts',(-19.9194162781616,17.4569855386215,
12.5846025120512));
#199356=CARTESIAN_POINT('Ctrl Pts',(-19.8494529408243,17.4101562300247,
12.5796125709236));
#199357=CARTESIAN_POINT('Ctrl Pts',(-19.7851860079688,17.3719013005707,
12.575386643219));
#199358=CARTESIAN_POINT('Ctrl Pts',(-19.5990860785352,17.2740759124247,
12.5637419663062));
#199359=CARTESIAN_POINT('Ctrl Pts',(-19.4733711743142,17.2226887999682,
12.5565299566913));
#199360=CARTESIAN_POINT('Ctrl Pts',(-19.2568625606815,17.1575862411018,
12.5440641699188));
#199361=CARTESIAN_POINT('Ctrl Pts',(-19.1685460712486,17.1371002164304,
12.5389719551515));
#199362=CARTESIAN_POINT('Ctrl Pts',(-19.0586647937198,17.1189400600132,
12.5324828739332));
#199363=CARTESIAN_POINT('Ctrl Pts',(-19.0380857978338,17.1158499331011,
12.5312613540816));
#199364=CARTESIAN_POINT('Ctrl Pts',(-19.0086348516524,17.111870633958,12.5295030791257));
#199365=CARTESIAN_POINT('Ctrl Pts',(-18.9997972453777,17.1107332984181,
12.5289741616074));
#199366=CARTESIAN_POINT('Ctrl Pts',(-18.9844923597262,17.1088618172458,
12.5280558443821));
#199367=CARTESIAN_POINT('Ctrl Pts',(-18.9780283432306,17.1081016363325,
12.5276672715735));
#199368=CARTESIAN_POINT('Ctrl Pts',(-18.965612626409,17.1066995401261,12.5269194990817));
#199369=CARTESIAN_POINT('Ctrl Pts',(-18.9596614994,17.1060530361355,12.5265604481554));
#199370=CARTESIAN_POINT('Ctrl Pts',(-18.9441079262473,17.1044300819816,
12.5256203752755));
#199371=CARTESIAN_POINT('Ctrl Pts',(-18.9345014838396,17.1034940544986,
12.5250380859469));
#199372=CARTESIAN_POINT('Ctrl Pts',(-18.9013560507739,17.1004931186363,
12.5230230691564));
#199373=CARTESIAN_POINT('Ctrl Pts',(-18.8777897678921,17.0987566959106,
12.5215800839237));
#199374=CARTESIAN_POINT('Ctrl Pts',(-18.6899012424729,17.0880714299837,
12.5099892867828));
#199375=CARTESIAN_POINT('Ctrl Pts',(-18.5251026446632,17.0979186449067,
12.4992323462443));
#199376=CARTESIAN_POINT('Ctrl Pts',(-18.2370095520701,17.149179824324,12.4798950751947));
#199377=CARTESIAN_POINT('Ctrl Pts',(-18.1131619060435,17.1830284032977,
12.4714194782576));
#199378=CARTESIAN_POINT('Ctrl Pts',(-17.9819496658706,17.2320478461235,
12.4627331353316));
#199379=CARTESIAN_POINT('Ctrl Pts',(-17.9708089840001,17.2363175393153,
12.4619981516652));
#199380=CARTESIAN_POINT('Ctrl Pts',(-17.9550266066247,17.2425196935959,
12.4609611649867));
#199381=CARTESIAN_POINT('Ctrl Pts',(-17.9503550170327,17.2443747672336,
12.4606547457596));
#199382=CARTESIAN_POINT('Ctrl Pts',(-17.9423172603459,17.2475997233052,
12.460128501367));
#199383=CARTESIAN_POINT('Ctrl Pts',(-17.9389479469103,17.2489616618302,
12.4599082021403));
#199384=CARTESIAN_POINT('Ctrl Pts',(-17.9324232046092,17.2516186500808,
12.4594821804507));
#199385=CARTESIAN_POINT('Ctrl Pts',(-17.9292673986513,17.2529126490303,
12.4592763940596));
#199386=CARTESIAN_POINT('Ctrl Pts',(-17.9207641087769,17.2564233465748,
12.4587225883768));
#199387=CARTESIAN_POINT('Ctrl Pts',(-17.915422521203,17.2586543794999,12.4583754303163));
#199388=CARTESIAN_POINT('Ctrl Pts',(-17.8956466524546,17.2670096410848,
12.4570926423709));
#199389=CARTESIAN_POINT('Ctrl Pts',(-17.8812709872245,17.2732724355222,
12.4561650528904));
#199390=CARTESIAN_POINT('Ctrl Pts',(-17.7430903583886,17.3353068164049,
12.4472842084464));
#199391=CARTESIAN_POINT('Ctrl Pts',(-17.6248348617212,17.4027163594933,
12.4399460763045));
#199392=CARTESIAN_POINT('Ctrl Pts',(-17.3869268745972,17.5705115265166,
12.4241364496277));
#199393=CARTESIAN_POINT('Ctrl Pts',(-17.2702647311286,17.6737036667616,
12.4156781380246));
#199394=CARTESIAN_POINT('Ctrl Pts',(-17.1516501821509,17.8044757174082,
12.4053962458497));
#199395=CARTESIAN_POINT('Ctrl Pts',(-17.1375974593144,17.8204460157528,
12.4041479530037));
#199396=CARTESIAN_POINT('Ctrl Pts',(-17.117952018687,17.8434625288588,12.4023578734839));
#199397=CARTESIAN_POINT('Ctrl Pts',(-17.1121595738175,17.8503371317314,
12.401824324488));
#199398=CARTESIAN_POINT('Ctrl Pts',(-17.1022400721328,17.8622631523878,
12.4009005352025));
#199399=CARTESIAN_POINT('Ctrl Pts',(-17.0980922228448,17.8672971721862,
12.4005111491311));
#199400=CARTESIAN_POINT('Ctrl Pts',(-17.0901933116631,17.8769744376842,
12.3997636115105));
#199401=CARTESIAN_POINT('Ctrl Pts',(-17.0864384881928,17.8816145430272,
12.3994056173556));
#199402=CARTESIAN_POINT('Ctrl Pts',(-17.076722222468,17.8937260239067,12.398472291294));
#199403=CARTESIAN_POINT('Ctrl Pts',(-17.0707917163883,17.9012219422236,
12.397895727346));
#199404=CARTESIAN_POINT('Ctrl Pts',(-17.0507243607571,17.9269423297956,
12.3959208854994));
#199405=CARTESIAN_POINT('Ctrl Pts',(-17.0368350628012,17.9453570456137,
12.3945128903651));
#199406=CARTESIAN_POINT('Ctrl Pts',(-16.9204468115025,18.105028527019,12.3823500964375));
#199407=CARTESIAN_POINT('Ctrl Pts',(-16.8354969553638,18.2582087384392,
12.3709003220424));
#199408=CARTESIAN_POINT('Ctrl Pts',(-16.7375521487364,18.5013704792442,
12.3535792629893));
#199409=CARTESIAN_POINT('Ctrl Pts',(-16.7098729182018,18.5846697592452,
12.3477984751274));
#199410=CARTESIAN_POINT('Ctrl Pts',(-16.6777196923027,18.7061794436123,
12.3397724386492));
#199411=CARTESIAN_POINT('Ctrl Pts',(-16.6689904029987,18.7431663997934,
12.337382282039));
#199412=CARTESIAN_POINT('Ctrl Pts',(-16.6597186930948,18.7877937404118,
12.3345774078427));
#199413=CARTESIAN_POINT('Ctrl Pts',(-16.6582163734147,18.7952250393248,
12.334112953271));
#199414=CARTESIAN_POINT('Ctrl Pts',(-16.6559468864146,18.8067701570194,
12.333395603268));
#199415=CARTESIAN_POINT('Ctrl Pts',(-16.6551519572504,18.8108783626274,
12.333141168883));
#199416=CARTESIAN_POINT('Ctrl Pts',(-16.6537025994971,18.8184895869389,
12.3326713460469));
#199417=CARTESIAN_POINT('Ctrl Pts',(-16.6530448407578,18.8219918710046,
12.3324557746841));
#199418=CARTESIAN_POINT('Ctrl Pts',(-16.651580614975,18.8298982414754,12.3319705026637));
#199419=CARTESIAN_POINT('Ctrl Pts',(-16.6507792761641,18.8343032225971,
12.3317010960942));
#199420=CARTESIAN_POINT('Ctrl Pts',(-16.6484632857467,18.847267719656,12.3309109264659));
#199421=CARTESIAN_POINT('Ctrl Pts',(-16.6469873492618,18.8558341798744,
12.3303923115206));
#199422=CARTESIAN_POINT('Ctrl Pts',(-16.6369266417622,18.9164565890559,
12.3267453933397));
#199423=CARTESIAN_POINT('Ctrl Pts',(-16.6302369607937,18.9688129747234,
12.323716234339));
#199424=CARTESIAN_POINT('Ctrl Pts',(-16.6241263825108,19.0367559453065,
12.3198779382673));
#199425=CARTESIAN_POINT('Ctrl Pts',(-16.6229109796364,19.0521578235637,
12.3190139730767));
#199426=CARTESIAN_POINT('Ctrl Pts',(-16.6088148094335,19.2597393350508,
12.3074364942488));
#199427=CARTESIAN_POINT('Ctrl Pts',(-16.6220498949103,19.4527862645305,
12.2973487796074));
#199428=CARTESIAN_POINT('Ctrl Pts',(-16.6722361451746,19.6944870069274,
12.2833673376024));
#199429=CARTESIAN_POINT('Ctrl Pts',(-16.6852965369748,19.7471373608193,
12.2802433641807));
#199430=CARTESIAN_POINT('Ctrl Pts',(-16.7038666652338,19.8113387842336,
12.2763119385533));
#199431=CARTESIAN_POINT('Ctrl Pts',(-16.7074785647983,19.8234205051229,
12.2755667300639));
#199432=CARTESIAN_POINT('Ctrl Pts',(-16.7133503992139,19.8424407556411,
12.2743847595165));
#199433=CARTESIAN_POINT('Ctrl Pts',(-16.7155386777619,19.8494012262096,
12.2739503480734));
#199434=CARTESIAN_POINT('Ctrl Pts',(-16.7197038804549,19.8624143725247,
12.273134619844));
#199435=CARTESIAN_POINT('Ctrl Pts',(-16.721672218605,19.8684697261473,12.272753589508));
#199436=CARTESIAN_POINT('Ctrl Pts',(-16.7261319786537,19.8819819825727,
12.2719000492049));
#199437=CARTESIAN_POINT('Ctrl Pts',(-16.7286376740101,19.8894340432063,
12.2714270719034));
#199438=CARTESIAN_POINT('Ctrl Pts',(-16.7350795554196,19.9082449875085,
12.2702273846959));
#199439=CARTESIAN_POINT('Ctrl Pts',(-16.7390710537003,19.9195845088839,
12.2694988503244));
#199440=CARTESIAN_POINT('Ctrl Pts',(-16.7621577476356,19.98343035874,12.2653661441093));
#199441=CARTESIAN_POINT('Ctrl Pts',(-16.7832275648349,20.0351944647441,
12.2618965246258));
#199442=CARTESIAN_POINT('Ctrl Pts',(-16.816529360096,20.1085553443587,12.2568019291525));
#199443=CARTESIAN_POINT('Ctrl Pts',(-16.8271330774761,20.1308683169119,
12.255228055829));
#199444=CARTESIAN_POINT('Ctrl Pts',(-16.9240137138269,20.3258530013913,
12.2412626563793));
#199445=CARTESIAN_POINT('Ctrl Pts',(-17.0331261948717,20.4861325231692,
12.2281887719511));
#199446=CARTESIAN_POINT('Ctrl Pts',(-17.1904552002863,20.6604508922759,
12.2131470363264));
#199447=CARTESIAN_POINT('Ctrl Pts',(-17.2193953186728,20.6906660564634,
12.2105091550339));
#199448=CARTESIAN_POINT('Ctrl Pts',(-17.2547639797147,20.7254670424927,
12.207454467003));
#199449=CARTESIAN_POINT('Ctrl Pts',(-17.2603442726056,20.7308975057357,
12.2069773127093));
#199450=CARTESIAN_POINT('Ctrl Pts',(-17.2690012142695,20.7392295112354,
12.2062446335026));
#199451=CARTESIAN_POINT('Ctrl Pts',(-17.2720567400587,20.7421527639776,
12.20598746481));
#199452=CARTESIAN_POINT('Ctrl Pts',(-17.2777011869994,20.747520564473,12.20551507117));
#199453=CARTESIAN_POINT('Ctrl Pts',(-17.2802874985051,20.7499677193296,
12.2052996473295));
#199454=CARTESIAN_POINT('Ctrl Pts',(-17.2861001113746,20.7554398567681,
12.2048177851147));
#199455=CARTESIAN_POINT('Ctrl Pts',(-17.2893297141327,20.7584612514064,
12.2045516222799));
#199456=CARTESIAN_POINT('Ctrl Pts',(-17.2975849567799,20.7661359209603,
12.2038751937367));
#199457=CARTESIAN_POINT('Ctrl Pts',(-17.3026237972977,20.770775008866,12.2034659879044));
#199458=CARTESIAN_POINT('Ctrl Pts',(-17.3315905409576,20.7971851154393,
12.2011339065317));
#199459=CARTESIAN_POINT('Ctrl Pts',(-17.3559938654293,20.8184311371059,
12.1992480505197));
#199460=CARTESIAN_POINT('Ctrl Pts',(-17.3956018123434,20.8513493296863,
12.1962923396516));
#199461=CARTESIAN_POINT('Ctrl Pts',(-17.4104933713668,20.8633879316851,
12.1952037595441));
#199462=CARTESIAN_POINT('Ctrl Pts',(-17.4266898551028,20.876122007533,12.1940414813639));
#199463=CARTESIAN_POINT('Ctrl Pts',(-17.4278340242785,20.8770196753955,
12.1939594895363));
#199464=CARTESIAN_POINT('Ctrl Pts',(-17.447019000192,20.8920395034338,12.1925865926441));
#199465=CARTESIAN_POINT('Ctrl Pts',(-17.4652874247353,20.9058694227012,
12.1913075409787));
#199466=CARTESIAN_POINT('Ctrl Pts',(-17.5206377176417,20.9463752660136,
12.1875043870956));
#199467=CARTESIAN_POINT('Ctrl Pts',(-17.5583626918446,20.9721509015813,
12.1850067597534));
#199468=CARTESIAN_POINT('Ctrl Pts',(-17.689129410271,21.0554218194558,12.1765663359542));
#199469=CARTESIAN_POINT('Ctrl Pts',(-17.7857771936881,21.1069216817362,
12.1706782404404));
#199470=CARTESIAN_POINT('Ctrl Pts',(-17.9364617815969,21.1727999192604,
12.1615338918867));
#199471=CARTESIAN_POINT('Ctrl Pts',(-17.987796765582,21.1928946038052,12.1584263684373));
#199472=CARTESIAN_POINT('Ctrl Pts',(-18.0722657029889,21.2222120073014,
12.1532823466898));
#199473=CARTESIAN_POINT('Ctrl Pts',(-18.1049439143532,21.2326711559176,
12.1512852362614));
#199474=CARTESIAN_POINT('Ctrl Pts',(-18.1482320484398,21.245375024352,12.1486245907639));
#199475=CARTESIAN_POINT('Ctrl Pts',(-18.1586265744733,21.2483392568301,
12.1479845839832));
#199476=CARTESIAN_POINT('Ctrl Pts',(-18.1756912044482,21.2530646105462,
12.146931876613));
#199477=CARTESIAN_POINT('Ctrl Pts',(-18.1823481042419,21.2548729826021,
12.146520717311));
#199478=CARTESIAN_POINT('Ctrl Pts',(-18.1952528754523,21.2583109745416,
12.1457226487722));
#199479=CARTESIAN_POINT('Ctrl Pts',(-18.2014996048667,21.2599446108758,
12.1453358749131));
#199480=CARTESIAN_POINT('Ctrl Pts',(-18.2159429949385,21.2636513152125,
12.1444404954634));
#199481=CARTESIAN_POINT('Ctrl Pts',(-18.2241447552368,21.265703898007,12.1439312337399));
#199482=CARTESIAN_POINT('Ctrl Pts',(-18.2462414749576,21.2710934017997,
12.1425569202425));
#199483=CARTESIAN_POINT('Ctrl Pts',(-18.2601581040461,21.2743388099902,
12.1416889403682));
#199484=CARTESIAN_POINT('Ctrl Pts',(-18.3881653422859,21.3028272449374,
12.1336815980427));
#199485=CARTESIAN_POINT('Ctrl Pts',(-18.5041113826693,21.3187206289427,
12.1262404516991));
#199486=CARTESIAN_POINT('Ctrl Pts',(-18.7832499910539,21.3336733342703,
12.1079811237119));
#199487=CARTESIAN_POINT('Ctrl Pts',(-18.9461969566186,21.3236145342229,
12.0970228873341));
#199488=CARTESIAN_POINT('Ctrl Pts',(-19.1383852166641,21.2892729526618,
12.084617373784));
#199489=CARTESIAN_POINT('Ctrl Pts',(-19.1702539702209,21.2828177070633,
12.0825798186054));
#199490=CARTESIAN_POINT('Ctrl Pts',(-19.2090239588168,21.274030211197,12.0801352718031));
#199491=CARTESIAN_POINT('Ctrl Pts',(-19.2160764625761,21.2723936308914,
12.0796919911676));
#199492=CARTESIAN_POINT('Ctrl Pts',(-19.2271190504475,21.2697713548855,
12.0790002604906));
#199493=CARTESIAN_POINT('Ctrl Pts',(-19.231114818645,21.2688101825384,12.0787504396736));
#199494=CARTESIAN_POINT('Ctrl Pts',(-19.2385781745122,21.2669918832874,
12.0782847559777));
#199495=CARTESIAN_POINT('Ctrl Pts',(-19.2420463537293,21.2661376258125,
12.0780687376301));
#199496=CARTESIAN_POINT('Ctrl Pts',(-19.2499579912323,21.2641676355279,
12.0775768110802));
#199497=CARTESIAN_POINT('Ctrl Pts',(-19.2543999916097,21.2630462562851,
12.0773012320426));
#199498=CARTESIAN_POINT('Ctrl Pts',(-19.2680410859687,21.2595554312031,
12.0764567366496));
#199499=CARTESIAN_POINT('Ctrl Pts',(-19.2772280462382,21.2571384443878,
12.0758904944011));
#199500=CARTESIAN_POINT('Ctrl Pts',(-19.3595522765203,21.2348863090597,
12.0708363810609));
#199501=CARTESIAN_POINT('Ctrl Pts',(-19.4316001034628,21.2111970235066,
12.066554286132));
#199502=CARTESIAN_POINT('Ctrl Pts',(-19.5420516518056,21.1681836503344,
12.0599934978968));
#199503=CARTESIAN_POINT('Ctrl Pts',(-19.5813962524043,21.1514729039001,
12.0576573597134));
#199504=CARTESIAN_POINT('Ctrl Pts',(-19.7194906370005,21.0878186822561,
12.0493787756542));
#199505=CARTESIAN_POINT('Ctrl Pts',(-19.8150773315717,21.0344338698914,
12.0434920757181));
#199506=CARTESIAN_POINT('Ctrl Pts',(-19.9519739052804,20.9434150514362,
12.0343509716056));
#199507=CARTESIAN_POINT('Ctrl Pts',(-19.99662744481,20.911145180756,12.0312453077688));
#199508=CARTESIAN_POINT('Ctrl Pts',(-20.0669593725278,20.8560180127472,
12.0261040899131));
#199509=CARTESIAN_POINT('Ctrl Pts',(-20.0934295932457,20.8342116115107,
12.0241078674788));
#199510=CARTESIAN_POINT('Ctrl Pts',(-20.1275293167234,20.8047006737721,
12.0214482373828));
#199511=CARTESIAN_POINT('Ctrl Pts',(-20.13564675635,20.7975661530511,12.0208083350939));
#199512=CARTESIAN_POINT('Ctrl Pts',(-20.1488551340384,20.7857766600723,
12.0197557558168));
#199513=CARTESIAN_POINT('Ctrl Pts',(-20.1539786398635,20.7811583487098,
12.0193446193799));
#199514=CARTESIAN_POINT('Ctrl Pts',(-20.1638543628842,20.7721685346796,
12.0185465639283));
#199515=CARTESIAN_POINT('Ctrl Pts',(-20.1686093355817,20.7678001623721,
12.0181597801255));
#199516=CARTESIAN_POINT('Ctrl Pts',(-20.1795448211767,20.7576611356858,
12.0172643320591));
#199517=CARTESIAN_POINT('Ctrl Pts',(-20.1857108626406,20.7518750977034,
12.0167550113461));
#199518=CARTESIAN_POINT('Ctrl Pts',(-20.2022061766497,20.7362094679103,
12.0153804354348));
#199519=CARTESIAN_POINT('Ctrl Pts',(-20.2124701917325,20.7262620811548,
12.0145122503961));
#199520=CARTESIAN_POINT('Ctrl Pts',(-20.3058953921581,20.6338659161811,
12.0064890871795));
#199521=CARTESIAN_POINT('Ctrl Pts',(-20.3821685714459,20.5447672374127,
11.9990309400375));
#199522=CARTESIAN_POINT('Ctrl Pts',(-20.5463777395271,20.3172193552303,
11.9806998495973));
#199523=CARTESIAN_POINT('Ctrl Pts',(-20.6263877497714,20.1739658026081,
11.9696847113564));
#199524=CARTESIAN_POINT('Ctrl Pts',(-20.7008875653749,19.9945721115513,
11.9573529102966));
#199525=CARTESIAN_POINT('Ctrl Pts',(-20.7120470405025,19.965958323262,11.9554288912061));
#199526=CARTESIAN_POINT('Ctrl Pts',(-20.7225806064515,19.9371103026709,
11.953538761502));
#199527=CARTESIAN_POINT('',(-20.8516474773841,19.2091064840258,12.4890562790225));
#199528=CARTESIAN_POINT('Ctrl Pts',(-20.8516474773841,19.2091064840258,
12.4890562790225));
#199529=CARTESIAN_POINT('Ctrl Pts',(-20.8529701850388,19.0661177649361,
12.4804472042752));
#199530=CARTESIAN_POINT('Ctrl Pts',(-20.7745205055235,18.2204815862945,
12.4294461939675));
#199531=CARTESIAN_POINT('Ctrl Pts',(-19.6371491691806,16.8763368280626,
12.336053248099));
#199532=CARTESIAN_POINT('Ctrl Pts',(-17.2597752565566,17.1878855805931,
12.2088774414178));
#199533=CARTESIAN_POINT('Ctrl Pts',(-16.2349110453346,19.3555162442872,
12.0817016347362));
#199534=CARTESIAN_POINT('Ctrl Pts',(-17.5028058390645,21.3905622235373,
11.9545258280549));
#199535=CARTESIAN_POINT('Ctrl Pts',(-19.6892758345617,21.4228771276963,
11.838541194803));
#199536=CARTESIAN_POINT('Ctrl Pts',(-20.5391741519826,20.4226738690892,
11.7649484971116));
#199537=CARTESIAN_POINT('Ctrl Pts',(-20.7219730492699,19.9368789336487,
11.7337477349808));
#199538=CARTESIAN_POINT('Ctrl Pts',(-20.8509991358365,19.209087183383,12.489429393495));
#199539=CARTESIAN_POINT('Ctrl Pts',(-20.8511371264887,19.3618075690115,
12.4977330855385));
#199540=CARTESIAN_POINT('Ctrl Pts',(-20.8347500521367,19.5140860427722,
12.5059642009009));
#199541=CARTESIAN_POINT('Ctrl Pts',(-20.7967940657989,19.6876464450794,
12.5161562698567));
#199542=CARTESIAN_POINT('Ctrl Pts',(-20.7910349565221,19.7119174639306,
12.5175993915336));
#199543=CARTESIAN_POINT('Ctrl Pts',(-20.7816382558835,19.7486189113664,
12.5198116649265));
#199544=CARTESIAN_POINT('Ctrl Pts',(-20.7783131362579,19.7611275404856,
12.5205709996961));
#199545=CARTESIAN_POINT('Ctrl Pts',(-20.7719302797975,19.7842816365704,
12.5219869115254));
#199546=CARTESIAN_POINT('Ctrl Pts',(-20.7689032850522,19.7949351621357,
12.5226424844955));
#199547=CARTESIAN_POINT('Ctrl Pts',(-20.7638390421021,19.8122411000255,
12.5237142877202));
#199548=CARTESIAN_POINT('Ctrl Pts',(-20.7618523246356,19.818908171434,12.5241288655344));
#199549=CARTESIAN_POINT('Ctrl Pts',(-20.7579646561404,19.8317233543802,
12.5249290164279));
#199550=CARTESIAN_POINT('Ctrl Pts',(-20.7560684601301,19.8378728364728,
12.5253144298941));
#199551=CARTESIAN_POINT('Ctrl Pts',(-20.7516570332761,19.8519510801957,
12.5262001515466));
#199552=CARTESIAN_POINT('Ctrl Pts',(-20.7491230627168,19.8598738168205,
12.5267010712896));
#199553=CARTESIAN_POINT('Ctrl Pts',(-20.7422545061787,19.8809207944706,
12.5280384508754));
#199554=CARTESIAN_POINT('Ctrl Pts',(-20.7378380266801,19.8940177018656,
12.528877598968));
#199555=CARTESIAN_POINT('Ctrl Pts',(-20.7297977044651,19.9171115879249,
12.5303698152429));
#199556=CARTESIAN_POINT('Ctrl Pts',(-20.7262265520042,19.9271252405564,
12.5310210574263));
#199557=CARTESIAN_POINT('Ctrl Pts',(-20.7225806018034,19.9371103154006,
12.5316746994897));
#199558=CARTESIAN_POINT('Origin',(-18.734,19.211,0.));
#199559=CARTESIAN_POINT('',(-20.722580608645,19.9371102966638,13.5571445218548));
#199560=CARTESIAN_POINT('',(-20.7225805710824,19.9371103995355,13.3344633171505));
#199561=CARTESIAN_POINT('',(-20.7225806064498,19.9371103026755,0.));
#199562=CARTESIAN_POINT('Ctrl Pts',(-20.722580608645,19.9371102966638,13.5571445218548));
#199563=CARTESIAN_POINT('Ctrl Pts',(-20.7282459073958,19.9215948807692,
13.5562052644303));
#199564=CARTESIAN_POINT('Ctrl Pts',(-20.7337298132394,19.9060126420946,
13.5552608856393));
#199565=CARTESIAN_POINT('Ctrl Pts',(-20.750223161395,19.8573354325802,13.5523054576032));
#199566=CARTESIAN_POINT('Ctrl Pts',(-20.7605967221015,19.8240341325958,
13.5502759196125));
#199567=CARTESIAN_POINT('Ctrl Pts',(-20.773119092699,19.780034764304,13.5475782150195));
#199568=CARTESIAN_POINT('Ctrl Pts',(-20.7760149188631,19.7695537589714,
13.5469344214741));
#199569=CARTESIAN_POINT('Ctrl Pts',(-20.7806193225015,19.7523742976286,
13.545877071117));
#199570=CARTESIAN_POINT('Ctrl Pts',(-20.7823760846193,19.7456888773732,
13.5454650823657));
#199571=CARTESIAN_POINT('Ctrl Pts',(-20.7857090367791,19.7327476847868,
13.544666531175));
#199572=CARTESIAN_POINT('Ctrl Pts',(-20.7872894372499,19.7264930684602,
13.5442801100892));
#199573=CARTESIAN_POINT('Ctrl Pts',(-20.7908666323442,19.7120584358001,
13.5433871819095));
#199574=CARTESIAN_POINT('Ctrl Pts',(-20.7928432517009,19.7038735751324,
13.5428800299894));
#199575=CARTESIAN_POINT('Ctrl Pts',(-20.7980153378751,19.6818826823534,
13.5415150903552));
#199576=CARTESIAN_POINT('Ctrl Pts',(-20.801121053926,19.6680561766484,13.5406544363613));
#199577=CARTESIAN_POINT('Ctrl Pts',(-20.835418189784,19.5078618821578,13.5306528589752));
#199578=CARTESIAN_POINT('Ctrl Pts',(-20.851137506266,19.3586426934896,13.521001335935));
#199579=CARTESIAN_POINT('Ctrl Pts',(-20.8508605240914,19.0592697719238,
13.5012717751918));
#199580=CARTESIAN_POINT('Ctrl Pts',(-20.8348287881357,18.9099266958755,
13.4912566176988));
#199581=CARTESIAN_POINT('Ctrl Pts',(-20.799845502621,18.748162883075,13.4809318733944));
#199582=CARTESIAN_POINT('Ctrl Pts',(-20.7963536195627,18.7328437297549,
13.4799597814493));
#199583=CARTESIAN_POINT('Ctrl Pts',(-20.7913410449669,18.7119304769614,
13.4786418129792));
#199584=CARTESIAN_POINT('Ctrl Pts',(-20.7899675523549,18.7063020808353,
13.4782880141239));
#199585=CARTESIAN_POINT('Ctrl Pts',(-20.7877485339382,18.6973682262046,
13.4777279559423));
#199586=CARTESIAN_POINT('Ctrl Pts',(-20.7869181049378,18.6940590995997,
13.4775208409079));
#199587=CARTESIAN_POINT('Ctrl Pts',(-20.785186732014,18.6872298278594,13.4770941107266));
#199588=CARTESIAN_POINT('Ctrl Pts',(-20.784284724454,18.683709992855,13.4768745642414));
#199589=CARTESIAN_POINT('Ctrl Pts',(-20.7821142198579,18.6753299779801,
13.4763527700331));
#199590=CARTESIAN_POINT('Ctrl Pts',(-20.7808374691826,18.6704719193154,
13.4760509980924));
#199591=CARTESIAN_POINT('Ctrl Pts',(-20.7764750782533,18.6541100545507,
13.4750369304475));
#199592=CARTESIAN_POINT('Ctrl Pts',(-20.7733095867119,18.6426275157399,
13.4743291031207));
#199593=CARTESIAN_POINT('Ctrl Pts',(-20.735765065069,18.5107911399019,13.4662399460591));
#199594=CARTESIAN_POINT('Ctrl Pts',(-20.6908688888608,18.3936696445328,
13.459408366111));
#199595=CARTESIAN_POINT('Ctrl Pts',(-20.5622080644684,18.1305007323441,
13.4434862170804));
#199596=CARTESIAN_POINT('Ctrl Pts',(-20.470900901101,17.9891196006906,13.4344327670586));
#199597=CARTESIAN_POINT('Ctrl Pts',(-20.3488895819459,17.8419229993028,
13.4233283739655));
#199598=CARTESIAN_POINT('Ctrl Pts',(-20.3336077748065,17.8240987426217,
13.4219533731892));
#199599=CARTESIAN_POINT('Ctrl Pts',(-20.3116466034115,17.7993297599487,
13.419997374714));
#199600=CARTESIAN_POINT('Ctrl Pts',(-20.3052111006416,17.7921704314923,
13.4194265313305));
#199601=CARTESIAN_POINT('Ctrl Pts',(-20.2946981094222,17.7806342461468,
13.4184976525528));
#199602=CARTESIAN_POINT('Ctrl Pts',(-20.2906504602041,17.7762302895008,
13.4181408833058));
#199603=CARTESIAN_POINT('Ctrl Pts',(-20.2821571001986,17.7670675211936,
13.4173940172811));
#199604=CARTESIAN_POINT('Ctrl Pts',(-20.277707991829,17.7623119574112,13.4170037770794));
#199605=CARTESIAN_POINT('Ctrl Pts',(-20.2671051402753,17.7510830843432,
13.4160760788625));
#199606=CARTESIAN_POINT('Ctrl Pts',(-20.2609322705816,17.7446280795804,
13.4155377970484));
#199607=CARTESIAN_POINT('Ctrl Pts',(-20.2401569273135,17.7231766119986,
13.4137320446068));
#199608=CARTESIAN_POINT('Ctrl Pts',(-20.2253732794107,17.7083580547387,
13.4124566646547));
#199609=CARTESIAN_POINT('Ctrl Pts',(-20.1447384548318,17.629895070409,13.4055489437137));
#199610=CARTESIAN_POINT('Ctrl Pts',(-20.0750377426678,17.5703629982089,
13.3997422941687));
#199611=CARTESIAN_POINT('Ctrl Pts',(-19.9260796328734,17.4589860280167,
13.3876785533894));
#199612=CARTESIAN_POINT('Ctrl Pts',(-19.8467533944115,17.4075630111075,
13.3814262633459));
#199613=CARTESIAN_POINT('Ctrl Pts',(-19.6994150670681,17.3254832687996,
13.3702890413442));
#199614=CARTESIAN_POINT('Ctrl Pts',(-19.6327063786031,17.2927904984049,
13.3654069071643));
#199615=CARTESIAN_POINT('Ctrl Pts',(-19.5255532053833,17.2470963944471,
13.357938199605));
#199616=CARTESIAN_POINT('Ctrl Pts',(-19.4862011994339,17.2316900806288,
13.355271086146));
#199617=CARTESIAN_POINT('Ctrl Pts',(-19.4393956549596,17.214963557571,13.3522082005009));
#199618=CARTESIAN_POINT('Ctrl Pts',(-19.4323664137032,17.2124933411401,
13.3517510810436));
#199619=CARTESIAN_POINT('Ctrl Pts',(-19.4209708585323,17.2085561798213,
13.3510148095728));
#199620=CARTESIAN_POINT('Ctrl Pts',(-19.4166126125033,17.2070663095747,
13.3507343516266));
#199621=CARTESIAN_POINT('Ctrl Pts',(-19.4088636482934,17.2044455323962,
13.3502377462513));
#199622=CARTESIAN_POINT('Ctrl Pts',(-19.4054748984273,17.2033089787763,
13.3500212686018));
#199623=CARTESIAN_POINT('Ctrl Pts',(-19.3981986887382,17.2008890925199,
13.3495579564602));
#199624=CARTESIAN_POINT('Ctrl Pts',(-19.3943103912965,17.1996084552503,
13.3493112814047));
#199625=CARTESIAN_POINT('Ctrl Pts',(-19.3836044811085,17.1961167810974,
13.3486345380573));
#199626=CARTESIAN_POINT('Ctrl Pts',(-19.3767792439967,17.193929050697,13.3482058205599));
#199627=CARTESIAN_POINT('Ctrl Pts',(-19.3399295113016,17.182323440626,13.3459051370449));
#199628=CARTESIAN_POINT('Ctrl Pts',(-19.3097072577266,17.1735406636963,
13.3440681326239));
#199629=CARTESIAN_POINT('Ctrl Pts',(-19.1212225221389,17.1232951591185,
13.3328547613254));
#199630=CARTESIAN_POINT('Ctrl Pts',(-18.9587779444252,17.0996165893947,
13.324209424332));
#199631=CARTESIAN_POINT('Ctrl Pts',(-18.6781394236988,17.0914986017331,
13.3088409293912));
#199632=CARTESIAN_POINT('Ctrl Pts',(-18.5610028530007,17.0978333525961,
13.302303466778));
#199633=CARTESIAN_POINT('Ctrl Pts',(-18.4308397129408,17.1157703822688,
13.2946060493309));
#199634=CARTESIAN_POINT('Ctrl Pts',(-18.416700193534,17.1178649999192,13.2937643190609));
#199635=CARTESIAN_POINT('Ctrl Pts',(-18.3942316652004,17.1214263641796,
13.2924174498814));
#199636=CARTESIAN_POINT('Ctrl Pts',(-18.3858882083006,17.1228001345264,
13.2919152541721));
#199637=CARTESIAN_POINT('Ctrl Pts',(-18.3711884695595,17.1253110283683,
13.291026765892));
#199638=CARTESIAN_POINT('Ctrl Pts',(-18.3648287049276,17.1264273228128,
13.2906411397131));
#199639=CARTESIAN_POINT('Ctrl Pts',(-18.3516858575842,17.1287962455108,
13.289841639869));
#199640=CARTESIAN_POINT('Ctrl Pts',(-18.3449035985754,17.1300529638296,
13.2894276400311));
#199641=CARTESIAN_POINT('Ctrl Pts',(-18.3275113951464,17.1333636499252,
13.2883622771834));
#199642=CARTESIAN_POINT('Ctrl Pts',(-18.3169109137869,17.1354657371154,
13.2877093854886));
#199643=CARTESIAN_POINT('Ctrl Pts',(-18.2727439680525,17.144576110914,13.2849739480399));
#199644=CARTESIAN_POINT('Ctrl Pts',(-18.2393357166929,17.1523179344066,
13.2828680842396));
#199645=CARTESIAN_POINT('Ctrl Pts',(-18.1527992406153,17.1745993531266,
13.2773138060491));
#199646=CARTESIAN_POINT('Ctrl Pts',(-18.1000269379603,17.1904062124275,
13.2738270096537));
#199647=CARTESIAN_POINT('Ctrl Pts',(-17.9444686966766,17.2436945681668,
13.2632580291975));
#199648=CARTESIAN_POINT('Ctrl Pts',(-17.8439124039957,17.2871000686388,
13.256027452449));
#199649=CARTESIAN_POINT('Ctrl Pts',(-17.7067682895232,17.3593603919983,
13.2457874379338));
#199650=CARTESIAN_POINT('Ctrl Pts',(-17.6670671255388,17.3819487003336,
13.2427765413148));
#199651=CARTESIAN_POINT('Ctrl Pts',(-17.6086447268562,17.4177385859405,
13.2383012730214));
#199652=CARTESIAN_POINT('Ctrl Pts',(-17.5893566555011,17.4299883053796,
13.2368162492262));
#199653=CARTESIAN_POINT('Ctrl Pts',(-17.5696842356408,17.4429337419373,
13.2352964308223));
#199654=CARTESIAN_POINT('Ctrl Pts',(-17.5690984633031,17.4433196267881,
13.2352511714255));
#199655=CARTESIAN_POINT('Ctrl Pts',(-17.5591293207858,17.4498940314335,
13.2344808304781));
#199656=CARTESIAN_POINT('Ctrl Pts',(-17.5497950416684,17.4561569955931,
13.2337583344831));
#199657=CARTESIAN_POINT('Ctrl Pts',(-17.5073067497728,17.4851585057362,
13.230465528539));
#199658=CARTESIAN_POINT('Ctrl Pts',(-17.4747523302698,17.5087658851297,
13.2279309371078));
#199659=CARTESIAN_POINT('Ctrl Pts',(-17.4370703308376,17.5377647151626,
13.2250016017706));
#199660=CARTESIAN_POINT('Ctrl Pts',(-17.4312761266593,17.5422719219111,
13.2245513024591));
#199661=CARTESIAN_POINT('Ctrl Pts',(-17.4219107699467,17.5496355722622,
13.2238238468773));
#199662=CARTESIAN_POINT('Ctrl Pts',(-17.418325279334,17.5524735637678,13.2235454339716));
#199663=CARTESIAN_POINT('Ctrl Pts',(-17.411956117236,17.5575485418906,13.2230510744505));
#199664=CARTESIAN_POINT('Ctrl Pts',(-17.4091688891385,17.5597809713361,
13.2228348089525));
#199665=CARTESIAN_POINT('Ctrl Pts',(-17.4031816373139,17.5646013780041,
13.2223704131566));
#199666=CARTESIAN_POINT('Ctrl Pts',(-17.3999835167876,17.5671916291267,
13.2221224503915));
#199667=CARTESIAN_POINT('Ctrl Pts',(-17.3911600059624,17.5743807577062,
13.2214385327544));
#199668=CARTESIAN_POINT('Ctrl Pts',(-17.3855506458471,17.5789993454052,
13.2210039766082));
#199669=CARTESIAN_POINT('Ctrl Pts',(-17.3546780548679,17.6046868028498,
13.2186128536975));
#199670=CARTESIAN_POINT('Ctrl Pts',(-17.3298832676818,17.62631467228,13.2166945800168));
#199671=CARTESIAN_POINT('Ctrl Pts',(-17.1857539564765,17.7580752175109,
13.2054867681597));
#199672=CARTESIAN_POINT('Ctrl Pts',(-17.078897780358,17.8810734656102,13.1969034242001));
#199673=CARTESIAN_POINT('Ctrl Pts',(-16.9212025345497,18.1114174523548,
13.1816207316834));
#199674=CARTESIAN_POINT('Ctrl Pts',(-16.8633460336548,18.2130195810622,
13.1751035442016));
#199675=CARTESIAN_POINT('Ctrl Pts',(-16.8081394607258,18.3318217758328,
13.1674289498601));
#199676=CARTESIAN_POINT('Ctrl Pts',(-16.8022494467284,18.3448401119813,
13.1665875123647));
#199677=CARTESIAN_POINT('Ctrl Pts',(-16.7930849391628,18.365654388574,13.1652410241529));
#199678=CARTESIAN_POINT('Ctrl Pts',(-16.78972452393,18.3734121860173,13.1647389140015));
#199679=CARTESIAN_POINT('Ctrl Pts',(-16.7838798137614,18.3871298954707,
13.1638505253839));
#199680=CARTESIAN_POINT('Ctrl Pts',(-16.7813761337724,18.3930814676722,
13.16346491283));
#199681=CARTESIAN_POINT('Ctrl Pts',(-16.7762539527176,18.4054151185397,
13.1626653904539));
#199682=CARTESIAN_POINT('Ctrl Pts',(-16.7736393439993,18.4117987215101,
13.1622513542088));
#199683=CARTESIAN_POINT('Ctrl Pts',(-16.7670078690167,18.4282179076416,
13.1611857907113));
#199684=CARTESIAN_POINT('Ctrl Pts',(-16.7630366189024,18.4382715929561,
13.1605327336622));
#199685=CARTESIAN_POINT('Ctrl Pts',(-16.7467811521142,18.4803648781251,
13.1577956937372));
#199686=CARTESIAN_POINT('Ctrl Pts',(-16.7352003966803,18.5126688750892,
13.1556883586312));
#199687=CARTESIAN_POINT('Ctrl Pts',(-16.70707472939,18.5975657355916,13.1501292744112));
#199688=CARTESIAN_POINT('Ctrl Pts',(-16.6917908493953,18.6505460653424,
13.1466390604284));
#199689=CARTESIAN_POINT('Ctrl Pts',(-16.6523927377921,18.8102868827723,
13.1360635151584));
#199690=CARTESIAN_POINT('Ctrl Pts',(-16.6344692945024,18.9183788325335,
13.1288298130631));
#199691=CARTESIAN_POINT('Ctrl Pts',(-16.6206804354889,19.0767390065439,
13.1183294300833));
#199692=CARTESIAN_POINT('Ctrl Pts',(-16.6181162941577,19.1262533336285,
13.1150620266067));
#199693=CARTESIAN_POINT('Ctrl Pts',(-16.6170162590124,19.1924272790692,
13.1107467113952));
#199694=CARTESIAN_POINT('Ctrl Pts',(-16.6169356878532,19.2090444000759,
13.1096674498783));
#199695=CARTESIAN_POINT('Ctrl Pts',(-16.6174195000452,19.2789033939328,
13.1051526981619));
#199696=CARTESIAN_POINT('Ctrl Pts',(-16.6197967557899,19.3321179478195,
13.1017682289513));
#199697=CARTESIAN_POINT('Ctrl Pts',(-16.6248955339115,19.3938750486984,
13.0979456663442));
#199698=CARTESIAN_POINT('Ctrl Pts',(-16.6256661577767,19.4025550783555,
13.0974108378647));
#199699=CARTESIAN_POINT('Ctrl Pts',(-16.6269142732002,19.4156920293778,
13.0966053368395));
#199700=CARTESIAN_POINT('Ctrl Pts',(-16.627352348132,19.420152477174,13.0963325309955));
#199701=CARTESIAN_POINT('Ctrl Pts',(-16.6281641899434,19.4281571825308,
13.0958442338215));
#199702=CARTESIAN_POINT('Ctrl Pts',(-16.6285327425798,19.4317019015688,
13.0956284548083));
#199703=CARTESIAN_POINT('Ctrl Pts',(-16.6293531076128,19.4394030150423,
13.0951606516315));
#199704=CARTESIAN_POINT('Ctrl Pts',(-16.6298082800898,19.4435589935281,
13.094908818839));
#199705=CARTESIAN_POINT('Ctrl Pts',(-16.6311216474387,19.4552311673385,
13.0942032185742));
#199706=CARTESIAN_POINT('Ctrl Pts',(-16.632007832681,19.4627442376995,13.0937509992246));
#199707=CARTESIAN_POINT('Ctrl Pts',(-16.6375516847289,19.5076733950392,
13.0910575238554));
#199708=CARTESIAN_POINT('Ctrl Pts',(-16.6431683078155,19.5449668737488,
13.0888668727374));
#199709=CARTESIAN_POINT('Ctrl Pts',(-16.6649490001153,19.6672968481861,
13.0817718359432));
#199710=CARTESIAN_POINT('Ctrl Pts',(-16.6853312226077,19.7514974222934,
13.077031836201));
#199711=CARTESIAN_POINT('Ctrl Pts',(-16.7626652808814,20.0025507386355,
13.0627369267368));
#199712=CARTESIAN_POINT('Ctrl Pts',(-16.8353145540425,20.1637329397712,
13.0532706872202));
#199713=CARTESIAN_POINT('Ctrl Pts',(-16.9390353979865,20.3336386538017,
13.0417029093244));
#199714=CARTESIAN_POINT('Ctrl Pts',(-16.9513079978244,20.3530265471152,
13.0403586266725));
#199715=CARTESIAN_POINT('Ctrl Pts',(-16.969125019228,20.3801861641347,13.0384390109132));
#199716=CARTESIAN_POINT('Ctrl Pts',(-16.974410859894,20.3881261774568,13.0378733220956));
#199717=CARTESIAN_POINT('Ctrl Pts',(-16.9830894024727,20.4009733889527,
13.0369505591202));
#199718=CARTESIAN_POINT('Ctrl Pts',(-16.9864495435496,20.4059025014566,
13.0365947179496));
#199719=CARTESIAN_POINT('Ctrl Pts',(-16.9935290003468,20.4161938790851,
13.0358479457907));
#199720=CARTESIAN_POINT('Ctrl Pts',(-16.997252361775,20.4215532728706,13.0354568631987));
#199721=CARTESIAN_POINT('Ctrl Pts',(-17.0061733991523,20.4342683099771,
13.0345237557428));
#199722=CARTESIAN_POINT('Ctrl Pts',(-17.0113933222732,20.4416081223215,
13.0339808811173));
#199723=CARTESIAN_POINT('Ctrl Pts',(-17.0291578474941,20.4662525842667,
13.0321436092435));
#199724=CARTESIAN_POINT('Ctrl Pts',(-17.0419173099536,20.4834000678817,
13.0308409206414));
#199725=CARTESIAN_POINT('Ctrl Pts',(-17.1129411707734,20.5758913795751,
13.0236779279189));
#199726=CARTESIAN_POINT('Ctrl Pts',(-17.1759722637987,20.6474210901233,
13.0176285599478));
#199727=CARTESIAN_POINT('Ctrl Pts',(-17.3647447806782,20.8345545074701,
13.0003560112373));
#199728=CARTESIAN_POINT('Ctrl Pts',(-17.4999563804146,20.9395607566476,
12.9888459807993));
#199729=CARTESIAN_POINT('Ctrl Pts',(-17.6778502601351,21.0460992780768,
12.9756116400919));
#199730=CARTESIAN_POINT('Ctrl Pts',(-17.7098920808618,21.0641716003169,
12.9732981934057));
#199731=CARTESIAN_POINT('Ctrl Pts',(-17.7487000691313,21.0847459923291,
12.9705933106989));
#199732=CARTESIAN_POINT('Ctrl Pts',(-17.755026463378,21.0880590868298,12.9701553906861));
#199733=CARTESIAN_POINT('Ctrl Pts',(-17.7653773241287,21.0934132041429,
12.9694439645255));
#199734=CARTESIAN_POINT('Ctrl Pts',(-17.7693917053173,21.0954734537915,
12.9691692891368));
#199735=CARTESIAN_POINT('Ctrl Pts',(-17.7765904065161,21.0991389213428,
12.9686789872335));
#199736=CARTESIAN_POINT('Ctrl Pts',(-17.7797722117947,21.1007489369777,
12.9684630626108));
#199737=CARTESIAN_POINT('Ctrl Pts',(-17.786672952114,21.1042188868042,12.9679964714297));
#199738=CARTESIAN_POINT('Ctrl Pts',(-17.7903932914092,21.1060759006419,
12.967745988007));
#199739=CARTESIAN_POINT('Ctrl Pts',(-17.8008038820364,21.1112341071183,
12.9670479702103));
#199740=CARTESIAN_POINT('Ctrl Pts',(-17.8075062238379,21.114510951618,12.9666019309341));
#199741=CARTESIAN_POINT('Ctrl Pts',(-17.8465891774246,21.1333636830468,
12.964019571208));
#199742=CARTESIAN_POINT('Ctrl Pts',(-17.8793469039137,21.1481495887896,
12.9619291200903));
#199743=CARTESIAN_POINT('Ctrl Pts',(-17.9859982380772,21.1930564458303,
12.9553091718838));
#199744=CARTESIAN_POINT('Ctrl Pts',(-18.0612266799572,21.2198385793404,
12.950919902283));
#199745=CARTESIAN_POINT('Ctrl Pts',(-18.3163865067015,21.294730178849,12.9364216409884));
#199746=CARTESIAN_POINT('Ctrl Pts',(-18.5010916551091,21.3233636582702,
12.9264692745726));
#199747=CARTESIAN_POINT('Ctrl Pts',(-18.7092084766712,21.3279697344123,
12.9143615696649));
#199748=CARTESIAN_POINT('Ctrl Pts',(-18.7312649157707,21.3281131149387,
12.9130685803715));
#199749=CARTESIAN_POINT('Ctrl Pts',(-18.76176960561,21.3278347285684,12.9112652848019));
#199750=CARTESIAN_POINT('Ctrl Pts',(-18.7702196015889,21.327707007685,12.910764164821));
#199751=CARTESIAN_POINT('Ctrl Pts',(-18.7847430870114,21.3274004951778,
12.9099000314596));
#199752=CARTESIAN_POINT('Ctrl Pts',(-18.7908170301856,21.3272461437095,
12.9095377866375));
#199753=CARTESIAN_POINT('Ctrl Pts',(-18.8033375603729,21.3268740293785,
12.9087892828695));
#199754=CARTESIAN_POINT('Ctrl Pts',(-18.8097839787012,21.3266529471114,
12.9084029236745));
#199755=CARTESIAN_POINT('Ctrl Pts',(-18.8247832047746,21.3260699020969,
12.9075016400214));
#199756=CARTESIAN_POINT('Ctrl Pts',(-18.8333349827925,21.3256855177204,
12.9069860176908));
#199757=CARTESIAN_POINT('Ctrl Pts',(-18.8607003270948,21.3242891424224,
12.9053302986479));
#199758=CARTESIAN_POINT('Ctrl Pts',(-18.8795024029744,21.3230778837619,
12.9041839820261));
#199759=CARTESIAN_POINT('Ctrl Pts',(-18.9733442061239,21.3157734599182,
12.8984176063806));
#199760=CARTESIAN_POINT('Ctrl Pts',(-19.048029803229,21.3059319997079,12.8936813032008));
#199761=CARTESIAN_POINT('Ctrl Pts',(-19.2293127889757,21.2721319244407,
12.8818311209907));
#199762=CARTESIAN_POINT('Ctrl Pts',(-19.334884623808,21.2438634398422,12.8746173490601));
#199763=CARTESIAN_POINT('Ctrl Pts',(-19.5501841534604,21.1679702634865,
12.8595366994744));
#199764=CARTESIAN_POINT('Ctrl Pts',(-19.6590387362335,21.1189305852053,
12.8516978038089));
#199765=CARTESIAN_POINT('Ctrl Pts',(-19.7715148752033,21.0563570054044,
12.8437479826082));
#199766=CARTESIAN_POINT('Ctrl Pts',(-19.7798013167007,21.0516735743813,
12.8431632938848));
#199767=CARTESIAN_POINT('Ctrl Pts',(-19.7920323210489,21.0446514471727,
12.8423020832976));
#199768=CARTESIAN_POINT('Ctrl Pts',(-19.7960011937486,21.0423556420021,
12.8420229105033));
#199769=CARTESIAN_POINT('Ctrl Pts',(-19.8029497390453,21.03830605235,12.8415346875896));
#199770=CARTESIAN_POINT('Ctrl Pts',(-19.8059326018198,21.0365578466142,
12.8413252816192));
#199771=CARTESIAN_POINT('Ctrl Pts',(-19.8123348112572,21.0327845172184,
12.8408762189911));
#199772=CARTESIAN_POINT('Ctrl Pts',(-19.815752733244,21.0307570763876,12.8406367161229));
#199773=CARTESIAN_POINT('Ctrl Pts',(-19.8228011823922,21.0265492060836,
12.8401432586166));
#199774=CARTESIAN_POINT('Ctrl Pts',(-19.8264309199432,21.0243674807774,
12.8398893885877));
#199775=CARTESIAN_POINT('Ctrl Pts',(-19.8355517791909,21.0188478837424,
12.8392520159915));
#199776=CARTESIAN_POINT('Ctrl Pts',(-19.8410343380238,21.0154958491952,
12.8388693998814));
#199777=CARTESIAN_POINT('Ctrl Pts',(-19.8566123030061,21.0058737682743,
12.8377834505836));
#199778=CARTESIAN_POINT('Ctrl Pts',(-19.866670459463,20.9995435054228,12.837083739143));
#199779=CARTESIAN_POINT('Ctrl Pts',(-19.9003600331289,20.9779422408574,
12.834743099242));
#199780=CARTESIAN_POINT('Ctrl Pts',(-19.923741079198,20.9622843639021,12.8331237184737));
#199781=CARTESIAN_POINT('Ctrl Pts',(-20.1088252450054,20.8329186129527,
12.8202871227201));
#199782=CARTESIAN_POINT('Ctrl Pts',(-20.2541976856571,20.69753256102,12.8100063819662));
#199783=CARTESIAN_POINT('Ctrl Pts',(-20.4249763388468,20.4868108874827,
12.7948508453257));
#199784=CARTESIAN_POINT('Ctrl Pts',(-20.468256540685,20.4273251921819,12.7906592706563));
#199785=CARTESIAN_POINT('Ctrl Pts',(-20.515479317361,20.3547618483329,12.7855790060097));
#199786=CARTESIAN_POINT('Ctrl Pts',(-20.5225045500718,20.3437449787257,
12.7848086283983));
#199787=CARTESIAN_POINT('Ctrl Pts',(-20.5337623764292,20.3257247795402,
12.7835496938018));
#199788=CARTESIAN_POINT('Ctrl Pts',(-20.5380572057999,20.318760597359,12.7830634392869));
#199789=CARTESIAN_POINT('Ctrl Pts',(-20.5456382811619,20.3063066570861,
12.7821942958995));
#199790=CARTESIAN_POINT('Ctrl Pts',(-20.5489402313534,20.3008265412692,
12.7818119892106));
#199791=CARTESIAN_POINT('Ctrl Pts',(-20.5558505420021,20.289239268294,12.7810038924124));
#199792=CARTESIAN_POINT('Ctrl Pts',(-20.5594531446599,20.2831287850949,
12.7805778985502));
#199793=CARTESIAN_POINT('Ctrl Pts',(-20.5689125005315,20.2668985864276,
12.7794467442218));
#199794=CARTESIAN_POINT('Ctrl Pts',(-20.5747161808223,20.2567483648043,
12.7787396750558));
#199795=CARTESIAN_POINT('Ctrl Pts',(-20.6014164502777,20.209140536072,12.7754244834299));
#199796=CARTESIAN_POINT('Ctrl Pts',(-20.6212544197464,20.1711036731717,
12.7727788948518));
#199797=CARTESIAN_POINT('Ctrl Pts',(-20.670727062303,20.0687794470757,12.7656650187975));
#199798=CARTESIAN_POINT('Ctrl Pts',(-20.6983134548541,20.0035701600995,
12.7611331539509));
#199799=CARTESIAN_POINT('Ctrl Pts',(-20.7225806071911,19.9371103006456,
12.75653014821));
#199800=CARTESIAN_POINT('Ctrl Pts',(-20.7225806018034,19.9371103154006,
12.5316746994897));
#199801=CARTESIAN_POINT('Ctrl Pts',(-20.6939757378795,20.0154497581957,
12.5368029489854));
#199802=CARTESIAN_POINT('Ctrl Pts',(-20.6607669422471,20.0920298936055,
12.5420833733886));
#199803=CARTESIAN_POINT('Ctrl Pts',(-20.602665918439,20.2069075948999,12.5504105413036));
#199804=CARTESIAN_POINT('Ctrl Pts',(-20.5809117602758,20.2466934439469,
12.5533735281679));
#199805=CARTESIAN_POINT('Ctrl Pts',(-20.5316283424972,20.3303296579239,
12.5597563757112));
#199806=CARTESIAN_POINT('Ctrl Pts',(-20.503733307023,20.3739318282504,12.5631796257824));
#199807=CARTESIAN_POINT('Ctrl Pts',(-20.4264177596365,20.4855481664746,
12.5721484126384));
#199808=CARTESIAN_POINT('Ctrl Pts',(-20.3744922025269,20.5517229657316,
12.5776795961887));
#199809=CARTESIAN_POINT('Ctrl Pts',(-20.2942311408303,20.6423410473356,
12.5854031239243));
#199810=CARTESIAN_POINT('Ctrl Pts',(-20.2689713883223,20.6693969381936,
12.5877297341331));
#199811=CARTESIAN_POINT('Ctrl Pts',(-20.2377192153322,20.7011592211483,
12.5904716532237));
#199812=CARTESIAN_POINT('Ctrl Pts',(-20.2323960249063,20.7065117316206,
12.5909340877451));
#199813=CARTESIAN_POINT('Ctrl Pts',(-20.2240794077151,20.7147851734803,
12.5916492914583));
#199814=CARTESIAN_POINT('Ctrl Pts',(-20.2211058256541,20.7177258387908,
12.5919035813813));
#199815=CARTESIAN_POINT('Ctrl Pts',(-20.2155821701284,20.7231560678198,
12.5923732706561));
#199816=CARTESIAN_POINT('Ctrl Pts',(-20.2130345465443,20.7256479824414,
12.59258885207));
#199817=CARTESIAN_POINT('Ctrl Pts',(-20.2072698478499,20.731258210957,12.5930743144939));
#199818=CARTESIAN_POINT('Ctrl Pts',(-20.2040491682681,20.7343727437133,
12.5933439003935));
#199819=CARTESIAN_POINT('Ctrl Pts',(-20.1945407447006,20.743509554752,12.5941350839851));
#199820=CARTESIAN_POINT('Ctrl Pts',(-20.1882256212846,20.7495033801158,
12.5946545252993));
#199821=CARTESIAN_POINT('Ctrl Pts',(-20.1431281644156,20.7917806114516,
12.5983229332164));
#199822=CARTESIAN_POINT('Ctrl Pts',(-20.1030260998331,20.826635500588,12.6013714207977));
#199823=CARTESIAN_POINT('Ctrl Pts',(-20.0473217756002,20.8714858909613,
12.6053941466042));
#199824=CARTESIAN_POINT('Ctrl Pts',(-20.0328414662831,20.8828368201011,
12.6064215426));
#199825=CARTESIAN_POINT('Ctrl Pts',(-19.8674199937629,21.0090619993885,
12.6179757194447));
#199826=CARTESIAN_POINT('Ctrl Pts',(-19.7018490214765,21.1033374937958,
12.627926805568));
#199827=CARTESIAN_POINT('Ctrl Pts',(-19.4760477215584,21.1944179954608,
12.6417205209282));
#199828=CARTESIAN_POINT('Ctrl Pts',(-19.4254231080912,21.2126281219504,
12.644819304011));
#199829=CARTESIAN_POINT('Ctrl Pts',(-19.3621221137179,21.2327099653548,
12.6487257231115));
#199830=CARTESIAN_POINT('Ctrl Pts',(-19.3500475104601,21.2364219383133,
12.6494722283799));
#199831=CARTESIAN_POINT('Ctrl Pts',(-19.3309427553344,21.2421084794397,
12.6506557923751));
#199832=CARTESIAN_POINT('Ctrl Pts',(-19.3239342474494,21.2441551564098,
12.6510904896425));
#199833=CARTESIAN_POINT('Ctrl Pts',(-19.3107946833903,21.2479186113388,
12.651906473571));
#199834=CARTESIAN_POINT('Ctrl Pts',(-19.3046661830549,21.2496440695109,
12.6522874720648));
#199835=CARTESIAN_POINT('Ctrl Pts',(-19.2909590858506,21.2534366046774,
12.6531405760855));
#199836=CARTESIAN_POINT('Ctrl Pts',(-19.2833766082406,21.2554891897882,
12.6536131467591));
#199837=CARTESIAN_POINT('Ctrl Pts',(-19.264182588152,21.2605705460335,12.6548111167751));
#199838=CARTESIAN_POINT('Ctrl Pts',(-19.2525565055725,21.2635428475853,
12.6555383314942));
#199839=CARTESIAN_POINT('Ctrl Pts',(-19.1869372681565,21.2797258398991,
12.6596522577984));
#199840=CARTESIAN_POINT('Ctrl Pts',(-19.1324697176687,21.2909037837291,
12.6631037295946));
#199841=CARTESIAN_POINT('Ctrl Pts',(-19.0530007504076,21.3039764680535,
12.6681954863541));
#199842=CARTESIAN_POINT('Ctrl Pts',(-19.0283033276721,21.307591866153,12.6697855034202));
#199843=CARTESIAN_POINT('Ctrl Pts',(-18.843488752511,21.3313166036231,12.6817366843576));
#199844=CARTESIAN_POINT('Ctrl Pts',(-18.6816101315199,21.3334930032669,
12.6925566367374));
#199845=CARTESIAN_POINT('Ctrl Pts',(-18.472333969205,21.3123378243056,12.7062829712044));
#199846=CARTESIAN_POINT('Ctrl Pts',(-18.4237672321485,21.3057186034452,
12.709445010742));
#199847=CARTESIAN_POINT('Ctrl Pts',(-18.3495878328167,21.29297166385,12.7141979600806));
#199848=CARTESIAN_POINT('Ctrl Pts',(-18.3237882155467,21.2880424073911,
12.715836551287));
#199849=CARTESIAN_POINT('Ctrl Pts',(-18.2914704780547,21.2812420923089,
12.7178652404337));
#199850=CARTESIAN_POINT('Ctrl Pts',(-18.2848618724701,21.2798184173128,
12.7182788199608));
#199851=CARTESIAN_POINT('Ctrl Pts',(-18.2743504604813,21.2775012288611,
12.718934505566));
#199852=CARTESIAN_POINT('Ctrl Pts',(-18.2704432385511,21.276628271881,12.7191777603174));
#199853=CARTESIAN_POINT('Ctrl Pts',(-18.263034204319,21.2749508542315,12.7196381033074));
#199854=CARTESIAN_POINT('Ctrl Pts',(-18.2595320080105,21.2741485729621,
12.719855306579));
#199855=CARTESIAN_POINT('Ctrl Pts',(-18.251471154613,21.272280386078,12.7203543421141));
#199856=CARTESIAN_POINT('Ctrl Pts',(-18.2469139805637,21.271208272795,12.7206358146928));
#199857=CARTESIAN_POINT('Ctrl Pts',(-18.2347012131966,21.2682923292672,
12.7213884653357));
#199858=CARTESIAN_POINT('Ctrl Pts',(-18.2270522043401,21.2664208677057,
12.7218580995142));
#199859=CARTESIAN_POINT('Ctrl Pts',(-18.1696272410509,21.2520308002749,
12.725371848381));
#199860=CARTESIAN_POINT('Ctrl Pts',(-18.1203065314138,21.2377472915025,
12.7283217401319));
#199861=CARTESIAN_POINT('Ctrl Pts',(-18.0580582235636,21.2172386438953,
12.732013863888));
#199862=CARTESIAN_POINT('Ctrl Pts',(-18.0446114803329,21.2126578787571,
12.7328095396516));
#199863=CARTESIAN_POINT('Ctrl Pts',(-17.8962877784859,21.1604579811881,
12.7415753146879));
#199864=CARTESIAN_POINT('Ctrl Pts',(-17.7665194593634,21.0994208882194,
12.7491693486816));
#199865=CARTESIAN_POINT('Ctrl Pts',(-17.5641903077008,20.9778839800793,
12.7621677102766));
#199866=CARTESIAN_POINT('Ctrl Pts',(-17.4877365417385,20.9248139374791,
12.7673878531307));
#199867=CARTESIAN_POINT('Ctrl Pts',(-17.3985178372785,20.853748203897,12.7740317061341));
#199868=CARTESIAN_POINT('Ctrl Pts',(-17.3822105066157,20.8403555126228,
12.7752701264902));
#199869=CARTESIAN_POINT('Ctrl Pts',(-17.3592676960378,20.8209317949007,
12.7770484849225));
#199870=CARTESIAN_POINT('Ctrl Pts',(-17.3524657852365,20.8150986570243,
12.777580334009));
#199871=CARTESIAN_POINT('Ctrl Pts',(-17.3407808116132,20.8049484844647,
12.7785021126087));
#199872=CARTESIAN_POINT('Ctrl Pts',(-17.3358802400462,20.8006517270705,
12.7788911979519));
#199873=CARTESIAN_POINT('Ctrl Pts',(-17.3265250460994,20.792372491627,12.7796388122746));
#199874=CARTESIAN_POINT('Ctrl Pts',(-17.3220672838421,20.7883936436532,
12.7799971870084));
#199875=CARTESIAN_POINT('Ctrl Pts',(-17.3104974181208,20.7779784324989,
12.7809329499628));
#199876=CARTESIAN_POINT('Ctrl Pts',(-17.3034121681018,20.7715125629169,
12.7815115829568));
#199877=CARTESIAN_POINT('Ctrl Pts',(-17.2792898127184,20.749196592085,12.7835010102009));
#199878=CARTESIAN_POINT('Ctrl Pts',(-17.262470699414,20.7331142974793,12.7849217166165));
#199879=CARTESIAN_POINT('Ctrl Pts',(-17.1239847155411,20.596254278873,12.7969092641665));
#199880=CARTESIAN_POINT('Ctrl Pts',(-17.0171596501688,20.4614063083084,
12.8081436431408));
#199881=CARTESIAN_POINT('Ctrl Pts',(-16.8808936944311,20.2385043294495,
12.8254075461086));
#199882=CARTESIAN_POINT('Ctrl Pts',(-16.8389404070292,20.1589025540898,
12.831338628619));
#199883=CARTESIAN_POINT('Ctrl Pts',(-16.7864092042904,20.0417011885649,
12.8395436730425));
#199884=CARTESIAN_POINT('Ctrl Pts',(-16.7716079683765,20.0061052247659,
12.8419691279139));
#199885=CARTESIAN_POINT('Ctrl Pts',(-16.755056309783,19.9630165006175,12.8448097554097));
#199886=CARTESIAN_POINT('Ctrl Pts',(-16.7523649797786,19.9558956953316,
12.8452761189057));
#199887=CARTESIAN_POINT('Ctrl Pts',(-16.7482515231648,19.9448321003641,
12.8459957749163));
#199888=CARTESIAN_POINT('Ctrl Pts',(-16.7468026291136,19.9408994277454,
12.8462506219511));
#199889=CARTESIAN_POINT('Ctrl Pts',(-16.744143577396,19.9336154665655,12.8467208276092));
#199890=CARTESIAN_POINT('Ctrl Pts',(-16.7429302115117,19.9302654536225,
12.8469363715683));
#199891=CARTESIAN_POINT('Ctrl Pts',(-16.7402141009249,19.9227069323436,
12.8474211056352));
#199892=CARTESIAN_POINT('Ctrl Pts',(-16.7387162248005,19.918496732264,12.8476900045509));
#199893=CARTESIAN_POINT('Ctrl Pts',(-16.7343571669519,19.9061204288711,
12.8484773069793));
#199894=CARTESIAN_POINT('Ctrl Pts',(-16.7315326666444,19.8979413767105,
12.848993585663));
#199895=CARTESIAN_POINT('Ctrl Pts',(-16.7121522154832,19.8406849939106,
12.8525812003558));
#199896=CARTESIAN_POINT('Ctrl Pts',(-16.697350646471,19.7910275918559,12.8555570257175));
#199897=CARTESIAN_POINT('Ctrl Pts',(-16.6790045187347,19.7200624691352,
12.8596845669602));
#199898=CARTESIAN_POINT('Ctrl Pts',(-16.6739416291031,19.6991706437737,
12.8608845964973));
#199899=CARTESIAN_POINT('Ctrl Pts',(-16.6387807428172,19.5437778278176,
12.8697221449241));
#199900=CARTESIAN_POINT('Ctrl Pts',(-16.6215631961414,19.4066993693504,
12.8770523915137));
#199901=CARTESIAN_POINT('Ctrl Pts',(-16.6153091995141,19.1781827269612,
12.8896557718727));
#199902=CARTESIAN_POINT('Ctrl Pts',(-16.6186640135761,19.0873933246637,
12.894758101716));
#199903=CARTESIAN_POINT('Ctrl Pts',(-16.6299381261798,18.9763798403343,
12.9012594161225));
#199904=CARTESIAN_POINT('Ctrl Pts',(-16.6323487137071,18.9556868327892,
12.9024822797136));
#199905=CARTESIAN_POINT('Ctrl Pts',(-16.6362262989008,18.926194860731,12.9042421523431));
#199906=CARTESIAN_POINT('Ctrl Pts',(-16.6374441722094,18.9173639571992,
12.9047713039514));
#199907=CARTESIAN_POINT('Ctrl Pts',(-16.6396477629919,18.9020985946339,
12.9056898972832));
#199908=CARTESIAN_POINT('Ctrl Pts',(-16.6406074560659,18.8956604584905,
12.9060785107318));
#199909=CARTESIAN_POINT('Ctrl Pts',(-16.6425065486055,18.8833111746527,
12.9068262693715));
#199910=CARTESIAN_POINT('Ctrl Pts',(-16.6434413555057,18.877399376094,12.9071852653646));
#199911=CARTESIAN_POINT('Ctrl Pts',(-16.645948341716,18.8619694297522,12.9081249890012));
#199912=CARTESIAN_POINT('Ctrl Pts',(-16.647560521134,18.8524580040773,12.9087069821842));
#199913=CARTESIAN_POINT('Ctrl Pts',(-16.653340563729,18.8197171295186,12.9107199333799));
#199914=CARTESIAN_POINT('Ctrl Pts',(-16.6578317032633,18.7965472193741,
12.9121611210903));
#199915=CARTESIAN_POINT('Ctrl Pts',(-16.6968550101441,18.61181384599,12.9237896471893));
#199916=CARTESIAN_POINT('Ctrl Pts',(-16.749799376812,18.4547514101852,12.9345914681778));
#199917=CARTESIAN_POINT('Ctrl Pts',(-16.8749454905301,18.1902934768021,
12.9539259743473));
#199918=CARTESIAN_POINT('Ctrl Pts',(-16.9397426723322,18.0802600403464,
12.9623536335936));
#199919=CARTESIAN_POINT('Ctrl Pts',(-17.0210403983306,17.9669734079629,
12.9710016530801));
#199920=CARTESIAN_POINT('Ctrl Pts',(-17.0281137715218,17.9572915213666,
12.9717403588792));
#199921=CARTESIAN_POINT('Ctrl Pts',(-17.0382747652153,17.9436285885701,
12.9727816451745));
#199922=CARTESIAN_POINT('Ctrl Pts',(-17.0412947731577,17.9395978674631,
12.9730886908595));
#199923=CARTESIAN_POINT('Ctrl Pts',(-17.0465196709674,17.9326759570553,
12.9736156695249));
#199924=CARTESIAN_POINT('Ctrl Pts',(-17.0487176679126,17.9297796124108,
12.9738360800628));
#199925=CARTESIAN_POINT('Ctrl Pts',(-17.0529903479878,17.9241794358584,
12.9742620488415));
#199926=CARTESIAN_POINT('Ctrl Pts',(-17.0550640982262,17.9214749507782,
12.9744676722848));
#199927=CARTESIAN_POINT('Ctrl Pts',(-17.0606692089384,17.9142014769428,
12.9750204735018));
#199928=CARTESIAN_POINT('Ctrl Pts',(-17.0642127777655,17.9096418709828,
12.9753667956314));
#199929=CARTESIAN_POINT('Ctrl Pts',(-17.0773898736568,17.8928289817404,
12.9766432338783));
#199930=CARTESIAN_POINT('Ctrl Pts',(-17.0871402490518,17.8806673586254,
12.977565411901));
#199931=CARTESIAN_POINT('Ctrl Pts',(-17.1836998002703,17.7629175844823,
12.9864951176728));
#199932=CARTESIAN_POINT('Ctrl Pts',(-17.2804210886076,17.6658488378552,
12.9938785515231));
#199933=CARTESIAN_POINT('Ctrl Pts',(-17.5049801053808,17.4803708958351,
13.0096951467069));
#199934=CARTESIAN_POINT('Ctrl Pts',(-17.634519212944,17.3953178864269,13.0181145403484));
#199935=CARTESIAN_POINT('Ctrl Pts',(-17.7911005572384,17.3154573192619,
13.0283509471637));
#199936=CARTESIAN_POINT('Ctrl Pts',(-17.810192476547,17.3060797852058,13.0295991178271));
#199937=CARTESIAN_POINT('Ctrl Pts',(-17.8375492481597,17.2931507212595,
13.0313890523388));
#199938=CARTESIAN_POINT('Ctrl Pts',(-17.8457008263835,17.2893615374382,
13.0319225803579));
#199939=CARTESIAN_POINT('Ctrl Pts',(-17.8598084695829,17.2829126799852,
13.0328463448206));
#199940=CARTESIAN_POINT('Ctrl Pts',(-17.865753192453,17.2802283860666,13.0332357271702));
#199941=CARTESIAN_POINT('Ctrl Pts',(-17.8771616969699,17.2751403065064,
13.033983265684));
#199942=CARTESIAN_POINT('Ctrl Pts',(-17.8826234337851,17.2727320691405,
13.0343412644924));
#199943=CARTESIAN_POINT('Ctrl Pts',(-17.8968576561934,17.2665275614899,
13.0352746203802));
#199944=CARTESIAN_POINT('Ctrl Pts',(-17.9056457256159,17.2627675807693,
13.0358512096565));
#199945=CARTESIAN_POINT('Ctrl Pts',(-17.9357274150561,17.2501374412311,
13.0378262304455));
#199946=CARTESIAN_POINT('Ctrl Pts',(-17.957139819771,17.2415560966169,13.039234381576));
#199947=CARTESIAN_POINT('Ctrl Pts',(-18.1416935628958,17.1710713823248,
13.0513951759771));
#199948=CARTESIAN_POINT('Ctrl Pts',(-18.3117420517259,17.1292193075748,
13.0628424756846));
#199949=CARTESIAN_POINT('Ctrl Pts',(-18.5720579118163,17.0983814302608,
13.0801628680898));
#199950=CARTESIAN_POINT('Ctrl Pts',(-18.65972397661,17.0934855447209,13.0859453644604));
#199951=CARTESIAN_POINT('Ctrl Pts',(-18.7854445246833,17.0942840444705,
13.093973440362));
#199952=CARTESIAN_POINT('Ctrl Pts',(-18.823432873117,17.095548475591,13.0963640022605));
#199953=CARTESIAN_POINT('Ctrl Pts',(-18.8689372367757,17.0982912112943,
13.0991692872839));
#199954=CARTESIAN_POINT('Ctrl Pts',(-18.8765029324068,17.0987880309988,
13.0996337639773));
#199955=CARTESIAN_POINT('Ctrl Pts',(-18.8882398333895,17.0996221126282,
13.1003511407098));
#199956=CARTESIAN_POINT('Ctrl Pts',(-18.8924128941211,17.0999311083808,
13.1006055798826));
#199957=CARTESIAN_POINT('Ctrl Pts',(-18.9001380732722,17.1005261575976,
13.101075407153));
#199958=CARTESIAN_POINT('Ctrl Pts',(-18.9036903550988,17.1008088042685,
13.1012909781908));
#199959=CARTESIAN_POINT('Ctrl Pts',(-18.9117040920276,17.1014668051293,
13.1017762439332));
#199960=CARTESIAN_POINT('Ctrl Pts',(-18.9161650672885,17.1018473422507,
13.1020456445837));
#199961=CARTESIAN_POINT('Ctrl Pts',(-18.9292829712635,17.1030082753133,
13.1028357807427));
#199962=CARTESIAN_POINT('Ctrl Pts',(-18.9379364606399,17.1038278484904,
13.1033543684103));
#199963=CARTESIAN_POINT('Ctrl Pts',(-18.9990565036251,17.1099965794217,
13.1070000432727));
#199964=CARTESIAN_POINT('Ctrl Pts',(-19.0513167497674,17.1172518317035,
13.1100280650202));
#199965=CARTESIAN_POINT('Ctrl Pts',(-19.1187991609385,17.1292056337981,
13.1138841932025));
#199966=CARTESIAN_POINT('Ctrl Pts',(-19.1343115325991,17.1321327911846,
13.11476686249));
#199967=CARTESIAN_POINT('Ctrl Pts',(-19.1996418870996,17.1452188985015,
13.1184736259121));
#199968=CARTESIAN_POINT('Ctrl Pts',(-19.2491196316764,17.1569975561323,
13.1212551272408));
#199969=CARTESIAN_POINT('Ctrl Pts',(-19.4035795587739,17.1997012889708,
13.1299803500712));
#199970=CARTESIAN_POINT('Ctrl Pts',(-19.5066125565614,17.2369867652113,
13.1358713302348));
#199971=CARTESIAN_POINT('Ctrl Pts',(-19.656577437648,17.3048035658457,13.1450223857008));
#199972=CARTESIAN_POINT('Ctrl Pts',(-19.7059453396827,17.3294964567632,
13.1481337539049));
#199973=CARTESIAN_POINT('Ctrl Pts',(-19.784378457078,17.3726384136937,13.1532835721569));
#199974=CARTESIAN_POINT('Ctrl Pts',(-19.8140584661585,17.3899174270098,
13.1552825178229));
#199975=CARTESIAN_POINT('Ctrl Pts',(-19.8525132495497,17.4135757253279,
13.1579452617814));
#199976=CARTESIAN_POINT('Ctrl Pts',(-19.8616788873658,17.4193119040908,
13.1585854843885));
#199977=CARTESIAN_POINT('Ctrl Pts',(-19.8766199764073,17.4288226279258,
13.1596384563426));
#199978=CARTESIAN_POINT('Ctrl Pts',(-19.8824217011921,17.4325556824806,
13.1600496628807));
#199979=CARTESIAN_POINT('Ctrl Pts',(-19.8936175175815,17.439837133579,13.1608477585023));
#199980=CARTESIAN_POINT('Ctrl Pts',(-19.8990138331243,17.4433819831007,
13.161234511866));
#199981=CARTESIAN_POINT('Ctrl Pts',(-19.9114372723222,17.4516245658215,
13.1621297497777));
#199982=CARTESIAN_POINT('Ctrl Pts',(-19.9184526096969,17.4563397876542,
13.1626388898059));
#199983=CARTESIAN_POINT('Ctrl Pts',(-19.9372457769357,17.4691353075703,
13.164012661985));
#199984=CARTESIAN_POINT('Ctrl Pts',(-19.9489702236747,17.4772928891142,
13.1648802186487));
#199985=CARTESIAN_POINT('Ctrl Pts',(-20.07557807645,17.567298531444,13.174365196308));
#199986=CARTESIAN_POINT('Ctrl Pts',(-20.182067377199,17.6602989408211,13.1834323132249));
#199987=CARTESIAN_POINT('Ctrl Pts',(-20.3445945702494,17.8336791733927,
13.1990666910339));
#199988=CARTESIAN_POINT('Ctrl Pts',(-20.4057792373794,17.9086245128324,
13.2054948616771));
#199989=CARTESIAN_POINT('Ctrl Pts',(-20.4993339042067,18.0407260570813,
13.2160580007295));
#199990=CARTESIAN_POINT('Ctrl Pts',(-20.5345602872609,18.0956842678464,
13.220252126317));
#199991=CARTESIAN_POINT('Ctrl Pts',(-20.5737749589651,18.1635792676172,
13.2251235692587));
#199992=CARTESIAN_POINT('Ctrl Pts',(-20.5802489425307,18.1750333246347,
13.2259351580403));
#199993=CARTESIAN_POINT('Ctrl Pts',(-20.5891459476138,18.1911226310708,
13.2270601566078));
#199994=CARTESIAN_POINT('Ctrl Pts',(-20.5916590611624,18.1957073582334,
13.2273790413168));
#199995=CARTESIAN_POINT('Ctrl Pts',(-20.595907904763,18.2035272053478,13.2279200092904));
#199996=CARTESIAN_POINT('Ctrl Pts',(-20.5976522423857,18.2067575999996,
13.2281426366694));
#199997=CARTESIAN_POINT('Ctrl Pts',(-20.6009776730976,18.2129545761209,
13.2285680661442));
#199998=CARTESIAN_POINT('Ctrl Pts',(-20.6025601088534,18.2159203951753,
13.2287709563414));
#199999=CARTESIAN_POINT('Ctrl Pts',(-20.6067291659775,18.2237791020038,
13.2293067057554));
#200000=CARTESIAN_POINT('Ctrl Pts',(-20.6093036963967,18.2286784241424,
13.2296388023647));
#200001=CARTESIAN_POINT('Ctrl Pts',(-20.6183487944788,18.2460563736321,
13.2308102280235));
#200002=CARTESIAN_POINT('Ctrl Pts',(-20.6247144240707,18.2585895991702,
13.2316432121907));
#200003=CARTESIAN_POINT('Ctrl Pts',(-20.7038353716376,18.4182901562788,
13.2421192697334));
#200004=CARTESIAN_POINT('Ctrl Pts',(-20.7593686000765,18.5733959132647,
13.2508474686791));
#200005=CARTESIAN_POINT('Ctrl Pts',(-20.8270296516777,18.8655648132127,
13.2671777503762));
#200006=CARTESIAN_POINT('Ctrl Pts',(-20.8448588515676,19.0003662911015,
13.2746744668283));
#200007=CARTESIAN_POINT('Ctrl Pts',(-20.8502665612874,19.152784629548,13.2835990378356));
#200008=CARTESIAN_POINT('Ctrl Pts',(-20.8506630230942,19.1696380610564,
13.2845915396842));
#200009=CARTESIAN_POINT('Ctrl Pts',(-20.8509528940655,19.1946775469274,
13.2860752297776));
#200010=CARTESIAN_POINT('Ctrl Pts',(-20.8510001744507,19.2028614086608,
13.2865616003627));
#200011=CARTESIAN_POINT('Ctrl Pts',(-20.8509998627497,19.21744352008,13.28743087348));
#200012=CARTESIAN_POINT('Ctrl Pts',(-20.8509707194948,19.2238416995252,
13.2878131931752));
#200013=CARTESIAN_POINT('Ctrl Pts',(-20.8508481156851,19.237331668986,13.2886212368629));
#200014=CARTESIAN_POINT('Ctrl Pts',(-20.8507480205181,19.2444233062069,
13.2890471641999));
#200015=CARTESIAN_POINT('Ctrl Pts',(-20.8503886243228,19.2631994798068,
13.2901779541959));
#200016=CARTESIAN_POINT('Ctrl Pts',(-20.8500681972047,19.2748824784275,
13.2908847233622));
#200017=CARTESIAN_POINT('Ctrl Pts',(-20.8481220038479,19.3293736724638,
13.2941963673929));
#200018=CARTESIAN_POINT('Ctrl Pts',(-20.8452939286926,19.3721263518761,
13.2968386108037));
#200019=CARTESIAN_POINT('Ctrl Pts',(-20.8339020511185,19.4899338561121,
13.3042463940272));
#200020=CARTESIAN_POINT('Ctrl Pts',(-20.8226163055533,19.564656190052,13.3090902071202));
#200021=CARTESIAN_POINT('Ctrl Pts',(-20.7864357642242,19.7400858175658,
13.3207653363176));
#200022=CARTESIAN_POINT('Ctrl Pts',(-20.7580935696955,19.8398518296155,
13.3276520160473));
#200023=CARTESIAN_POINT('Ctrl Pts',(-20.7225805710824,19.9371103995355,
13.3344633171505));
#200024=CARTESIAN_POINT('Origin',(-18.734,19.211,0.));
#200025=CARTESIAN_POINT('',(-20.7249099185723,19.937940853899,14.355439970105));
#200026=CARTESIAN_POINT('',(-20.7225805809329,19.9371103725581,14.1348941200942));
#200027=CARTESIAN_POINT('',(-20.7225806064498,19.9371103026755,0.));
#200028=CARTESIAN_POINT('',(-20.8478642240166,19.211459512885,14.3110922513879));
#200029=CARTESIAN_POINT('Ctrl Pts',(-20.8476071148151,19.2114685807671,
14.310944106499));
#200030=CARTESIAN_POINT('Ctrl Pts',(-20.8480884069697,19.4590066998217,
14.3257760610343));
#200031=CARTESIAN_POINT('Ctrl Pts',(-20.80739811974,19.7063940898195,14.3406080155697));
#200032=CARTESIAN_POINT('Ctrl Pts',(-20.7249099185723,19.937940853899,14.355439970105));
#200033=CARTESIAN_POINT('Ctrl Pts',(-20.8509999712459,19.2113489194644,
14.3128990514644));
#200034=CARTESIAN_POINT('Ctrl Pts',(-20.8510014361084,19.2024611552748,
14.3123784859613));
#200035=CARTESIAN_POINT('Ctrl Pts',(-20.8509469309422,19.1935735497784,
14.3118562320931));
#200036=CARTESIAN_POINT('Ctrl Pts',(-20.8507292584551,19.1760624133584,
14.3108237614325));
#200037=CARTESIAN_POINT('Ctrl Pts',(-20.8505693533197,19.1674390332335,
14.3103136564554));
#200038=CARTESIAN_POINT('Ctrl Pts',(-20.8502036147191,19.1526059869016,
14.3094332672318));
#200039=CARTESIAN_POINT('Ctrl Pts',(-20.8500231310319,19.1463957633363,
14.3090637777332));
#200040=CARTESIAN_POINT('Ctrl Pts',(-20.8496088606873,19.1340179085138,
14.3083255149905));
#200041=CARTESIAN_POINT('Ctrl Pts',(-20.8493754334206,19.1278503261407,
14.3079567565876));
#200042=CARTESIAN_POINT('Ctrl Pts',(-20.848855723496,19.1155429558949,14.3072190705556));
#200043=CARTESIAN_POINT('Ctrl Pts',(-20.8485696657352,19.1094032186219,
14.3068501535266));
#200044=CARTESIAN_POINT('Ctrl Pts',(-20.8477228781531,19.0927853673251,
14.3058491347497));
#200045=CARTESIAN_POINT('Ctrl Pts',(-20.8471109809795,19.082310136904,14.30521543353));
#200046=CARTESIAN_POINT('Ctrl Pts',(-20.8445147257632,19.042899487298,14.3028208683896));
#200047=CARTESIAN_POINT('Ctrl Pts',(-20.8420137560137,19.0140023769774,
14.3010439012303));
#200048=CARTESIAN_POINT('Ctrl Pts',(-20.8144782635763,18.7573526849457,
14.2850653343867));
#200049=CARTESIAN_POINT('Ctrl Pts',(-20.753211591893,18.5350388691164,14.269604433014));
#200050=CARTESIAN_POINT('Ctrl Pts',(-20.6340839915613,18.2758348938444,
14.2510838378801));
#200051=CARTESIAN_POINT('Ctrl Pts',(-20.6085646358542,18.2256769524415,
14.2474877607192));
#200052=CARTESIAN_POINT('Ctrl Pts',(-20.5751286687195,18.1659725642482,
14.2432425645308));
#200053=CARTESIAN_POINT('Ctrl Pts',(-20.5690903961147,18.1554052054487,
14.2424925974347));
#200054=CARTESIAN_POINT('Ctrl Pts',(-20.560409458869,18.1405126516654,14.2414383174952));
#200055=CARTESIAN_POINT('Ctrl Pts',(-20.5578420111671,18.1361441985472,
14.2411293897551));
#200056=CARTESIAN_POINT('Ctrl Pts',(-20.5534026131307,18.1286523709495,
14.2406002011725));
#200057=CARTESIAN_POINT('Ctrl Pts',(-20.5515382512226,18.1255245443153,
14.2403794522541));
#200058=CARTESIAN_POINT('Ctrl Pts',(-20.5479175144887,18.1194855429855,
14.2399536264843));
#200059=CARTESIAN_POINT('Ctrl Pts',(-20.5461621961086,18.1165737874974,
14.2397484806425));
#200060=CARTESIAN_POINT('Ctrl Pts',(-20.5414281368992,18.1087634562195,
14.2391986301067));
#200061=CARTESIAN_POINT('Ctrl Pts',(-20.5384364741632,18.1038726898179,
14.2388547647149));
#200062=CARTESIAN_POINT('Ctrl Pts',(-20.5273808238152,18.0859627814456,
14.2375969485602));
#200063=CARTESIAN_POINT('Ctrl Pts',(-20.5191952827764,18.073018736953,14.2366906394999));
#200064=CARTESIAN_POINT('Ctrl Pts',(-20.4329200664155,17.9398113524507,
14.2273801595364));
#200065=CARTESIAN_POINT('Ctrl Pts',(-20.3429326823567,17.8276716575317,
14.2196650392277));
#200066=CARTESIAN_POINT('Ctrl Pts',(-20.143065965183,17.6247417878619,14.204193749349));
#200067=CARTESIAN_POINT('Ctrl Pts',(-20.0340165922372,17.5342076098945,
14.1964684471925));
#200068=CARTESIAN_POINT('Ctrl Pts',(-19.9021332799011,17.4453655951087,
14.1872528265992));
#200069=CARTESIAN_POINT('Ctrl Pts',(-19.8873798999456,17.4356929869136,
14.1862240528257));
#200070=CARTESIAN_POINT('Ctrl Pts',(-19.8639721957415,17.4207613745174,
14.1845942123657));
#200071=CARTESIAN_POINT('Ctrl Pts',(-19.8553978859257,17.4153780254611,
14.1839976996536));
#200072=CARTESIAN_POINT('Ctrl Pts',(-19.8408083615995,17.406363301082,14.1829833922676));
#200073=CARTESIAN_POINT('Ctrl Pts',(-19.8348130293989,17.4026999593859,
14.1825667722271));
#200074=CARTESIAN_POINT('Ctrl Pts',(-19.8230017557086,17.395563395887,14.1817463193197));
#200075=CARTESIAN_POINT('Ctrl Pts',(-19.8171871566711,17.3920881083811,
14.1813425682413));
#200076=CARTESIAN_POINT('Ctrl Pts',(-19.8059706291668,17.3854570371514,
14.1805639657056));
#200077=CARTESIAN_POINT('Ctrl Pts',(-19.800571187759,17.3822971703578,14.1801892682528));
#200078=CARTESIAN_POINT('Ctrl Pts',(-19.7879859654366,17.3750067316828,
14.1793161207764));
#200079=CARTESIAN_POINT('Ctrl Pts',(-19.7807898114373,17.3708943551351,
14.1788170194299));
#200080=CARTESIAN_POINT('Ctrl Pts',(-19.7616178673035,17.3600870472655,
14.1774876453664));
#200081=CARTESIAN_POINT('Ctrl Pts',(-19.7496009762144,17.3534661825408,
14.1766547350752));
#200082=CARTESIAN_POINT('Ctrl Pts',(-19.6575661445073,17.3039184250284,
14.1702772305848));
#200083=CARTESIAN_POINT('Ctrl Pts',(-19.5749355579623,17.2660685982982,
14.1645541765244));
#200084=CARTESIAN_POINT('Ctrl Pts',(-19.3564459783098,17.1825183701739,
14.149447690927));
#200085=CARTESIAN_POINT('Ctrl Pts',(-19.2179152282854,17.1450867253631,
14.1398743484975));
#200086=CARTESIAN_POINT('Ctrl Pts',(-19.0250550073876,17.1134506217828,
14.1270950656102));
#200087=CARTESIAN_POINT('Ctrl Pts',(-18.9731248713825,17.106897710058,14.1237108504651));
#200088=CARTESIAN_POINT('Ctrl Pts',(-18.8936566373678,17.0998504524788,
14.1186666159142));
#200089=CARTESIAN_POINT('Ctrl Pts',(-18.8662650649588,17.0979574606686,
14.1169522408766));
#200090=CARTESIAN_POINT('Ctrl Pts',(-18.8319910100657,17.0962579763324,
14.1148437913913));
#200091=CARTESIAN_POINT('Ctrl Pts',(-18.8251373351981,17.0959515244726,
14.1144240031113));
#200092=CARTESIAN_POINT('Ctrl Pts',(-18.8142595621251,17.0955181140307,
14.1137607740516));
#200093=CARTESIAN_POINT('Ctrl Pts',(-18.8102364521885,17.0953693112551,
14.1135161394941));
#200094=CARTESIAN_POINT('Ctrl Pts',(-18.8026275322974,17.0951096125571,
14.1130547382518));
#200095=CARTESIAN_POINT('Ctrl Pts',(-18.7990419100372,17.0949963563436,
14.1128378478732));
#200096=CARTESIAN_POINT('Ctrl Pts',(-18.7908167627642,17.0947574818597,
14.1123415337505));
#200097=CARTESIAN_POINT('Ctrl Pts',(-18.7861771046747,17.0946380057271,
14.112062456411));
#200098=CARTESIAN_POINT('Ctrl Pts',(-18.7738027239945,17.0943600700649,
14.1113204025284));
#200099=CARTESIAN_POINT('Ctrl Pts',(-18.7660673796609,17.0942287470952,
14.1108589024566));
#200100=CARTESIAN_POINT('Ctrl Pts',(-18.7105206704841,17.0935902888748,
14.1075607924631));
#200101=CARTESIAN_POINT('Ctrl Pts',(-18.6627010439702,17.0946606180976,
14.1048058391841));
#200102=CARTESIAN_POINT('Ctrl Pts',(-18.5863863887302,17.0989588134262,
14.1004866742263));
#200103=CARTESIAN_POINT('Ctrl Pts',(-18.5578524533513,17.101146948829,14.0988891270869));
#200104=CARTESIAN_POINT('Ctrl Pts',(-18.4860611086704,17.1081189464573,
14.0948948962025));
#200105=CARTESIAN_POINT('Ctrl Pts',(-18.4428902215796,17.1136593708419,
14.0925160463929));
#200106=CARTESIAN_POINT('Ctrl Pts',(-18.2919610675702,17.1377794793268,
14.0841946673857));
#200107=CARTESIAN_POINT('Ctrl Pts',(-18.1855021437519,17.1633694276856,
14.0783076130399));
#200108=CARTESIAN_POINT('Ctrl Pts',(-18.0290972439073,17.2140434629985,
14.0691656850162));
#200109=CARTESIAN_POINT('Ctrl Pts',(-17.9773802934524,17.2330593332276,
14.0660595489563));
#200110=CARTESIAN_POINT('Ctrl Pts',(-17.8947632612499,17.2671515186741,
14.0609176190743));
#200111=CARTESIAN_POINT('Ctrl Pts',(-17.8633843627988,17.2810017000321,
14.0589211711253));
#200112=CARTESIAN_POINT('Ctrl Pts',(-17.8225786124641,17.300210409725,14.0562612831552));
#200113=CARTESIAN_POINT('Ctrl Pts',(-17.8128357915825,17.3048881726049,
14.0556213543255));
#200114=CARTESIAN_POINT('Ctrl Pts',(-17.7969340937783,17.3126733505018,
14.0545687425131));
#200115=CARTESIAN_POINT('Ctrl Pts',(-17.7907537556867,17.3157366669364,
14.0541576002687));
#200116=CARTESIAN_POINT('Ctrl Pts',(-17.7788173466281,17.3217258560732,
14.0533595414941));
#200117=CARTESIAN_POINT('Ctrl Pts',(-17.7730594671969,17.3246479694405,
14.052972760218));
#200118=CARTESIAN_POINT('Ctrl Pts',(-17.7597926517222,17.3314573595997,
14.0520773295852));
#200119=CARTESIAN_POINT('Ctrl Pts',(-17.7522934943752,17.3353633539261,
14.0515680238594));
#200120=CARTESIAN_POINT('Ctrl Pts',(-17.7321817606472,17.3459923621472,
14.0501935146202));
#200121=CARTESIAN_POINT('Ctrl Pts',(-17.7196137044144,17.352798261342,14.0493253817085));
#200122=CARTESIAN_POINT('Ctrl Pts',(-17.604967392435,17.4163916537719,14.041320236642));
#200123=CARTESIAN_POINT('Ctrl Pts',(-17.5077005723999,17.481400144653,14.0338816548519));
#200124=CARTESIAN_POINT('Ctrl Pts',(-17.2890242455132,17.655307404964,14.0156317693971));
#200125=CARTESIAN_POINT('Ctrl Pts',(-17.1738359726383,17.7708532554101,
14.0046806493747));
#200126=CARTESIAN_POINT('Ctrl Pts',(-17.0527786490054,17.9240467969068,
13.9922725077672));
#200127=CARTESIAN_POINT('Ctrl Pts',(-17.0331405496458,17.9501149221383,
13.9902271697918));
#200128=CARTESIAN_POINT('Ctrl Pts',(-17.0098856677209,17.9825166655757,
13.987774602756));
#200129=CARTESIAN_POINT('Ctrl Pts',(-17.0056897218789,17.9884268448191,
13.9873308091675));
#200130=CARTESIAN_POINT('Ctrl Pts',(-16.9991612511879,17.9977232713858,
13.9866384570032));
#200131=CARTESIAN_POINT('Ctrl Pts',(-16.9968081429046,18.0010948975714,
13.9863885236746));
#200132=CARTESIAN_POINT('Ctrl Pts',(-16.9924293000988,18.0074081864139,
13.9859227423806));
#200133=CARTESIAN_POINT('Ctrl Pts',(-16.9904012094102,18.0103480878408,
13.9857067382689));
#200134=CARTESIAN_POINT('Ctrl Pts',(-16.9857901705053,18.0170685299058,
13.9852149892101));
#200135=CARTESIAN_POINT('Ctrl Pts',(-16.98321204571,18.0208523187268,13.9849395725074));
#200136=CARTESIAN_POINT('Ctrl Pts',(-16.9753306568642,18.0325004823382,
13.9840960687318));
#200137=CARTESIAN_POINT('Ctrl Pts',(-16.9700678716026,18.0403922836419,
13.9835306466567));
#200138=CARTESIAN_POINT('Ctrl Pts',(-16.8985026535371,18.149286346342,13.9758077734178));
#200139=CARTESIAN_POINT('Ctrl Pts',(-16.8409021112143,18.2557642630198,
13.9691788512222));
#200140=CARTESIAN_POINT('Ctrl Pts',(-16.7212417796211,18.5308637742304,
13.9528531364415));
#200141=CARTESIAN_POINT('Ctrl Pts',(-16.6709342707907,18.7035221969101,
13.9432269751985));
#200142=CARTESIAN_POINT('Ctrl Pts',(-16.6396109529109,18.9016698411859,
13.931546709493));
#200143=CARTESIAN_POINT('Ctrl Pts',(-16.6365795287003,18.9229410749684,
13.9302860809617));
#200144=CARTESIAN_POINT('Ctrl Pts',(-16.6327352125529,18.9532079221095,
13.9284813669376));
#200145=CARTESIAN_POINT('Ctrl Pts',(-16.6316552496936,18.9621687129683,
13.9279457068064));
#200146=CARTESIAN_POINT('Ctrl Pts',(-16.6298928385996,18.9776232975215,
13.927019416919));
#200147=CARTESIAN_POINT('Ctrl Pts',(-16.6291830660321,18.9841138943763,
13.9266296538938));
#200148=CARTESIAN_POINT('Ctrl Pts',(-16.6278827007965,18.9965368039438,
13.9258821966779));
#200149=CARTESIAN_POINT('Ctrl Pts',(-16.6272871174503,19.0024685399363,
13.9255246637581));
#200150=CARTESIAN_POINT('Ctrl Pts',(-16.6258058221287,19.0178759935954,
13.9245943025838));
#200151=CARTESIAN_POINT('Ctrl Pts',(-16.6249589458899,19.0273552317331,
13.924020257734));
#200152=CARTESIAN_POINT('Ctrl Pts',(-16.6222991901077,19.0595762244486,
13.9220632342899));
#200153=CARTESIAN_POINT('Ctrl Pts',(-16.6207900662452,19.08234082903,13.9206707744085));
#200154=CARTESIAN_POINT('Ctrl Pts',(-16.610755260275,19.2827379019803,13.9083226741322));
#200155=CARTESIAN_POINT('Ctrl Pts',(-16.6242786936108,19.4607322600714,
13.8966418568998));
#200156=CARTESIAN_POINT('Ctrl Pts',(-16.6769703053261,19.7185506508725,
13.8792575885286));
#200157=CARTESIAN_POINT('Ctrl Pts',(-16.6991126331987,19.8010966920309,
13.8736345038582));
#200158=CARTESIAN_POINT('Ctrl Pts',(-16.7380394344089,19.9175618845139,
13.8657971684818));
#200159=CARTESIAN_POINT('Ctrl Pts',(-16.7508364498547,19.9527216506691,
13.8634448258777));
#200160=CARTESIAN_POINT('Ctrl Pts',(-16.7673280142462,19.9945478734847,
13.8606783139092));
#200161=CARTESIAN_POINT('Ctrl Pts',(-16.7701341729209,20.0015548600593,
13.8602159435152));
#200162=CARTESIAN_POINT('Ctrl Pts',(-16.7745514351743,20.0124161026467,
13.8595011119499));
#200163=CARTESIAN_POINT('Ctrl Pts',(-16.7761365392633,20.0162807694132,
13.8592471287445));
#200164=CARTESIAN_POINT('Ctrl Pts',(-16.7790953530739,20.0234343202682,
13.8587777222644));
#200165=CARTESIAN_POINT('Ctrl Pts',(-16.7804659177088,20.0267243976635,
13.8585621187336));
#200166=CARTESIAN_POINT('Ctrl Pts',(-16.7835806055966,20.0341484170485,
13.8580762485064));
#200167=CARTESIAN_POINT('Ctrl Pts',(-16.7853295608258,20.0382802734836,
13.8578062791063));
#200168=CARTESIAN_POINT('Ctrl Pts',(-16.7905227264005,20.050441131481,13.8570129250961));
#200169=CARTESIAN_POINT('Ctrl Pts',(-16.794003565405,20.0584545214519,13.8564917146073));
#200170=CARTESIAN_POINT('Ctrl Pts',(-16.8191828177947,20.1154525671578,
13.8527940658262));
#200171=CARTESIAN_POINT('Ctrl Pts',(-16.8426861647177,20.1636239002871,
13.8497198783941));
#200172=CARTESIAN_POINT('Ctrl Pts',(-16.8687418804884,20.2122510445528,
13.846617966454));
#200173=CARTESIAN_POINT('Ctrl Pts',(-16.8694912047369,20.2136457295714,
13.8465290012217));
#200174=CARTESIAN_POINT('Ctrl Pts',(-16.9499448449609,20.3629885559826,
13.8370026142969));
#200175=CARTESIAN_POINT('Ctrl Pts',(-17.0469830877593,20.5009270442499,
13.8281568217718));
#200176=CARTESIAN_POINT('Ctrl Pts',(-17.1986287364124,20.6696922788584,
13.8155775117368));
#200177=CARTESIAN_POINT('Ctrl Pts',(-17.2397418358419,20.7117797506953,
13.8122701236083));
#200178=CARTESIAN_POINT('Ctrl Pts',(-17.3087280757825,20.7767528411853,
13.8068257553542));
#200179=CARTESIAN_POINT('Ctrl Pts',(-17.3355272421349,20.8007344865888,
13.8047344763484));
#200180=CARTESIAN_POINT('Ctrl Pts',(-17.3713000663059,20.83114158881,13.8019663225418));
#200181=CARTESIAN_POINT('Ctrl Pts',(-17.3797323372157,20.8381966592026,
13.8013154720447));
#200182=CARTESIAN_POINT('Ctrl Pts',(-17.3935755057102,20.8495967547373,
13.8002494647671));
#200183=CARTESIAN_POINT('Ctrl Pts',(-17.3989535550439,20.8539814781596,
13.7998359263978));
#200184=CARTESIAN_POINT('Ctrl Pts',(-17.4093653563391,20.8623853433021,
13.7990364339964));
#200185=CARTESIAN_POINT('Ctrl Pts',(-17.4143960922524,20.8664081117642,
13.7986506323148));
#200186=CARTESIAN_POINT('Ctrl Pts',(-17.4259965408285,20.875597791774,13.7977620949432));
#200187=CARTESIAN_POINT('Ctrl Pts',(-17.432578618685,20.8807488561788,13.7972587346905));
#200188=CARTESIAN_POINT('Ctrl Pts',(-17.4502337558508,20.8943977707451,
13.7959105854448));
#200189=CARTESIAN_POINT('Ctrl Pts',(-17.4613605031513,20.9028252039088,
13.7950630392939));
#200190=CARTESIAN_POINT('Ctrl Pts',(-17.5524254343221,20.9703913757237,
13.7881422545663));
#200191=CARTESIAN_POINT('Ctrl Pts',(-17.636344870651,21.0239326422511,13.7818535544323));
#200192=CARTESIAN_POINT('Ctrl Pts',(-17.8752652868229,21.153680747242,13.7642222294857));
#200193=CARTESIAN_POINT('Ctrl Pts',(-18.0363028913904,21.2171525569805,
13.7525823078525));
#200194=CARTESIAN_POINT('Ctrl Pts',(-18.2419618706716,21.2704141600095,
13.7389940113692));
#200195=CARTESIAN_POINT('Ctrl Pts',(-18.2809540346393,21.2793418563952,
13.7364749385332));
#200196=CARTESIAN_POINT('Ctrl Pts',(-18.3277213637619,21.2886635495839,
13.7335397442831));
#200197=CARTESIAN_POINT('Ctrl Pts',(-18.3352725227154,21.2901259121459,
13.7330684823386));
#200198=CARTESIAN_POINT('Ctrl Pts',(-18.346967287639,21.2923246714394,13.7323429118898));
#200199=CARTESIAN_POINT('Ctrl Pts',(-18.3511053107049,21.2930899034384,
13.7320870086122));
#200200=CARTESIAN_POINT('Ctrl Pts',(-18.358749955898,21.2944800432895,13.7316158145563));
#200201=CARTESIAN_POINT('Ctrl Pts',(-18.3622558463511,21.2951084355035,
13.7314003322577));
#200202=CARTESIAN_POINT('Ctrl Pts',(-18.3701428439712,21.296501557907,13.7309169365973));
#200203=CARTESIAN_POINT('Ctrl Pts',(-18.3745247710316,21.2972613303741,
13.7306493071747));
#200204=CARTESIAN_POINT('Ctrl Pts',(-18.3857402754254,21.2991695764505,
13.7299666399164));
#200205=CARTESIAN_POINT('Ctrl Pts',(-18.3925772171162,21.3002983276923,
13.7295526957684));
#200206=CARTESIAN_POINT('Ctrl Pts',(-18.4324961258276,21.3066875941387,
13.7271480225704));
#200207=CARTESIAN_POINT('Ctrl Pts',(-18.4656956689786,21.3111962162708,
13.7251970334994));
#200208=CARTESIAN_POINT('Ctrl Pts',(-18.517213677266,21.3169508367706,13.7222257543013));
#200209=CARTESIAN_POINT('Ctrl Pts',(-18.5354632608623,21.3187496139726,
13.721184070428));
#200210=CARTESIAN_POINT('Ctrl Pts',(-18.5848602084064,21.3229711683156,
13.7183883942142));
#200211=CARTESIAN_POINT('Ctrl Pts',(-18.6160421535645,21.3249420445597,
13.7166492099635));
#200212=CARTESIAN_POINT('Ctrl Pts',(-18.6857207844649,21.3277994823183,
13.7127984913676));
#200213=CARTESIAN_POINT('Ctrl Pts',(-18.7242210427121,21.3283274266283,
13.7106949694213));
#200214=CARTESIAN_POINT('Ctrl Pts',(-18.871990195673,21.3263228986546,13.7026493649938));
#200215=CARTESIAN_POINT('Ctrl Pts',(-18.9809854365671,21.3163810967737,
13.6967644339791));
#200216=CARTESIAN_POINT('Ctrl Pts',(-19.1429757713918,21.2888489755441,
13.6876274419331));
#200217=CARTESIAN_POINT('Ctrl Pts',(-19.1968464670634,21.2775164048774,
13.6845241347417));
#200218=CARTESIAN_POINT('Ctrl Pts',(-19.283449812941,21.2557416712581,13.6793864704477));
#200219=CARTESIAN_POINT('Ctrl Pts',(-19.3164783870537,21.2465791145829,
13.6773913736653));
#200220=CARTESIAN_POINT('Ctrl Pts',(-19.3596071730437,21.2334790258985,
13.6747330307718));
#200221=CARTESIAN_POINT('Ctrl Pts',(-19.3699213050779,21.2302597238493,
13.6740932610015));
#200222=CARTESIAN_POINT('Ctrl Pts',(-19.3867782972178,21.2248562677711,
13.6730408441732));
#200223=CARTESIAN_POINT('Ctrl Pts',(-19.3933360067944,21.2227188175719,
13.6726297367327));
#200224=CARTESIAN_POINT('Ctrl Pts',(-19.4060125452849,21.2185183272665,
13.6718316978604));
#200225=CARTESIAN_POINT('Ctrl Pts',(-19.412132617633,21.2164592608179,13.6714449014303));
#200226=CARTESIAN_POINT('Ctrl Pts',(-19.4262461205299,21.2116388549707,
13.6705493662661));
#200227=CARTESIAN_POINT('Ctrl Pts',(-19.4342325760768,21.2088575663861,
13.6700399706809));
#200228=CARTESIAN_POINT('Ctrl Pts',(-19.4556758291152,21.2012455669553,
13.6686650616762));
#200229=CARTESIAN_POINT('Ctrl Pts',(-19.4691005277455,21.196326325187,13.6677966162071));
#200230=CARTESIAN_POINT('Ctrl Pts',(-19.5923288068216,21.1497503007377,
13.6597527064958));
#200231=CARTESIAN_POINT('Ctrl Pts',(-19.6985198484934,21.0991669976578,
13.6522722506534));
#200232=CARTESIAN_POINT('Ctrl Pts',(-19.9414512566245,20.9575884534316,
13.6339020086518));
#200233=CARTESIAN_POINT('Ctrl Pts',(-20.0728962327269,20.8589887583509,
13.6228709691785));
#200234=CARTESIAN_POINT('Ctrl Pts',(-20.2141768510264,20.7248459152367,
13.6105089203488));
#200235=CARTESIAN_POINT('Ctrl Pts',(-20.2362207476064,20.7029738693543,
13.6085649811454));
#200236=CARTESIAN_POINT('Ctrl Pts',(-20.2627314377079,20.675486302712,13.6062171643345));
#200237=CARTESIAN_POINT('Ctrl Pts',(-20.2676601523895,20.6703239804051,
13.6057802354619));
#200238=CARTESIAN_POINT('Ctrl Pts',(-20.2753701244454,20.6621663736319,
13.6050962036969));
#200239=CARTESIAN_POINT('Ctrl Pts',(-20.2781689230392,20.6591878477137,
13.604847778877));
#200240=CARTESIAN_POINT('Ctrl Pts',(-20.2833998752318,20.6535885795356,
13.6043832907146));
#200241=CARTESIAN_POINT('Ctrl Pts',(-20.2858339874894,20.6509698117177,
13.6041670803481));
#200242=CARTESIAN_POINT('Ctrl Pts',(-20.2913956817454,20.6449557174504,
13.6036728812598));
#200243=CARTESIAN_POINT('Ctrl Pts',(-20.2945187951976,20.6415563253114,
13.6033952334243));
#200244=CARTESIAN_POINT('Ctrl Pts',(-20.3041550095504,20.6309985589258,
13.6025380427304));
#200245=CARTESIAN_POINT('Ctrl Pts',(-20.3106302672645,20.6238056022485,
13.6019612919911));
#200246=CARTESIAN_POINT('Ctrl Pts',(-20.3791741512318,20.5466063575582,
13.5958448863841));
#200247=CARTESIAN_POINT('Ctrl Pts',(-20.4365943402133,20.472593958169,13.5906201605121));
#200248=CARTESIAN_POINT('Ctrl Pts',(-20.5627793897382,20.2855640012514,
13.578242942316));
#200249=CARTESIAN_POINT('Ctrl Pts',(-20.6262219468887,20.1694457514907,
13.5711935484779));
#200250=CARTESIAN_POINT('Ctrl Pts',(-20.6941947322286,20.0115708805455,
13.5616457046566));
#200251=CARTESIAN_POINT('Ctrl Pts',(-20.7089153611662,19.9745349775608,
13.5594101014325));
#200252=CARTESIAN_POINT('Ctrl Pts',(-20.722580608645,19.9371102966638,13.5571445218548));
#200253=CARTESIAN_POINT('',(-20.8509992001769,19.2129106825237,14.0892704698819));
#200254=CARTESIAN_POINT('Ctrl Pts',(-20.7225805710824,19.9371103995355,
13.3344633171505));
#200255=CARTESIAN_POINT('Ctrl Pts',(-20.714099989437,19.9603359584895,13.336089870733));
#200256=CARTESIAN_POINT('Ctrl Pts',(-20.7052104669082,19.9834185567835,
13.3377116194092));
#200257=CARTESIAN_POINT('Ctrl Pts',(-20.6896745200346,20.0217416997203,
13.3404079023461));
#200258=CARTESIAN_POINT('Ctrl Pts',(-20.6832526751649,20.0370623226433,
13.3414868207997));
#200259=CARTESIAN_POINT('Ctrl Pts',(-20.6554930751894,20.1011617266236,
13.3460010150011));
#200260=CARTESIAN_POINT('Ctrl Pts',(-20.6324975938024,20.1492065098487,
13.3493852707072));
#200261=CARTESIAN_POINT('Ctrl Pts',(-20.6036571521101,20.2040493757279,
13.353207619908));
#200262=CARTESIAN_POINT('Ctrl Pts',(-20.5995537730845,20.2117367559937,
13.3537424368348));
#200263=CARTESIAN_POINT('Ctrl Pts',(-20.5932681278435,20.2233394269715,
13.354547923945));
#200264=CARTESIAN_POINT('Ctrl Pts',(-20.5911207589636,20.2272733756704,
13.3548207273185));
#200265=CARTESIAN_POINT('Ctrl Pts',(-20.5872434542799,20.2343232138439,
13.3553090218582));
#200266=CARTESIAN_POINT('Ctrl Pts',(-20.5855181368739,20.2374415668869,
13.3555248006939));
#200267=CARTESIAN_POINT('Ctrl Pts',(-20.5817516686177,20.2442087157465,
13.3559926055366));
#200268=CARTESIAN_POINT('Ctrl Pts',(-20.5797075877119,20.2478558147259,
13.3562444401614));
#200269=CARTESIAN_POINT('Ctrl Pts',(-20.5739344739495,20.2580851744219,
13.3569500507283));
#200270=CARTESIAN_POINT('Ctrl Pts',(-20.5701809002478,20.2646536131018,
13.3574022784752));
#200271=CARTESIAN_POINT('Ctrl Pts',(-20.5475082460105,20.3038397277491,
13.3600959089861));
#200272=CARTESIAN_POINT('Ctrl Pts',(-20.5277543971108,20.3359695052267,
13.362286700065));
#200273=CARTESIAN_POINT('Ctrl Pts',(-20.4598655160041,20.4400519771557,
13.3693824172442));
#200274=CARTESIAN_POINT('Ctrl Pts',(-20.408174207836,20.509585243042,13.3741229213973));
#200275=CARTESIAN_POINT('Ctrl Pts',(-20.2388262196164,20.7104019699307,
13.3884175678289));
#200276=CARTESIAN_POINT('Ctrl Pts',(-20.1089430818994,20.8303310563656,
13.3978831230899));
#200277=CARTESIAN_POINT('Ctrl Pts',(-19.9470525241611,20.9461423837107,
13.4094501372104));
#200278=CARTESIAN_POINT('Ctrl Pts',(-19.9281749115875,20.9591881300637,
13.4107944810016));
#200279=CARTESIAN_POINT('Ctrl Pts',(-19.9011551667847,20.9772187871638,
13.4127141691007));
#200280=CARTESIAN_POINT('Ctrl Pts',(-19.8931852369537,20.9824597284118,
13.4132798681161));
#200281=CARTESIAN_POINT('Ctrl Pts',(-19.8801738311297,20.9908904843162,
13.4142026431836));
#200282=CARTESIAN_POINT('Ctrl Pts',(-19.8751537551993,20.9941132025755,
13.4145584861831));
#200283=CARTESIAN_POINT('Ctrl Pts',(-19.8646136993918,21.0008168200143,
13.4153052584736));
#200284=CARTESIAN_POINT('Ctrl Pts',(-19.8590911190167,21.0042934949104,
13.415696339352));
#200285=CARTESIAN_POINT('Ctrl Pts',(-19.8459085367891,21.0125075697508,
13.4166294358663));
#200286=CARTESIAN_POINT('Ctrl Pts',(-19.8382342505364,21.0172217012531,
13.4171723012111));
#200287=CARTESIAN_POINT('Ctrl Pts',(-19.8122482612514,21.0329567678506,
13.4190095089672));
#200288=CARTESIAN_POINT('Ctrl Pts',(-19.7938002763088,21.043749054994,13.4203121419455));
#200289=CARTESIAN_POINT('Ctrl Pts',(-19.6922717085249,21.1010989660828,
13.4274746095074));
#200290=CARTESIAN_POINT('Ctrl Pts',(-19.6062958858279,21.1422831036723,
13.4335234769039));
#200291=CARTESIAN_POINT('Ctrl Pts',(-19.3593924826863,21.2406973185158,
13.4507950654043));
#200292=CARTESIAN_POINT('Ctrl Pts',(-19.1938926996427,21.2844711270082,
13.462304652001));
#200293=CARTESIAN_POINT('Ctrl Pts',(-18.988496630972,21.3129690980325,13.4755396085012));
#200294=CARTESIAN_POINT('Ctrl Pts',(-18.9519258567018,21.3170748615545,
13.4778539234984));
#200295=CARTESIAN_POINT('Ctrl Pts',(-18.9081483700512,21.3208370445699,
13.4805596920531));
#200296=CARTESIAN_POINT('Ctrl Pts',(-18.9010293445624,21.3214125688606,
13.480997663745));
#200297=CARTESIAN_POINT('Ctrl Pts',(-18.8894079323888,21.3222929062983,
13.4817091568979));
#200298=CARTESIAN_POINT('Ctrl Pts',(-18.8849073101776,21.3226193658521,
13.4819838479591));
#200299=CARTESIAN_POINT('Ctrl Pts',(-18.8768482013101,21.3231780482486,
13.482474166745));
#200300=CARTESIAN_POINT('Ctrl Pts',(-18.873290153154,21.3234156716807,13.4826900926648));
#200301=CARTESIAN_POINT('Ctrl Pts',(-18.8655821738045,21.3239108876134,
13.4831566740311));
#200302=CARTESIAN_POINT('Ctrl Pts',(-18.8614320922034,21.3241652443711,
13.4834071464096));
#200303=CARTESIAN_POINT('Ctrl Pts',(-18.849834436901,21.3248417696012,13.484105102238));
#200304=CARTESIAN_POINT('Ctrl Pts',(-18.8423852568591,21.3252368087648,
13.4845510910201));
#200305=CARTESIAN_POINT('Ctrl Pts',(-18.7990570790752,21.3273049553139,
13.4871325677332));
#200306=CARTESIAN_POINT('Ctrl Pts',(-18.763139931681,21.3281042245254,13.4892222229809));
#200307=CARTESIAN_POINT('Ctrl Pts',(-18.6474865241204,21.327733690139,13.4958384900428));
#200308=CARTESIAN_POINT('Ctrl Pts',(-18.5678270879652,21.3229741107929,
13.5002250538236));
#200309=CARTESIAN_POINT('Ctrl Pts',(-18.3036688515648,21.2921480309304,
13.5147250553068));
#200310=CARTESIAN_POINT('Ctrl Pts',(-18.1223943214257,21.2462627739796,
13.5246812615265));
#200311=CARTESIAN_POINT('Ctrl Pts',(-17.9289826328832,21.1690914577697,
13.5367932104503));
#200312=CARTESIAN_POINT('Ctrl Pts',(-17.9086339339583,21.1606014776153,
13.538085731516));
#200313=CARTESIAN_POINT('Ctrl Pts',(-17.8806756847399,21.1484204526868,
13.5398884767732));
#200314=CARTESIAN_POINT('Ctrl Pts',(-17.8729496384795,21.1449991389044,
13.5403895221042));
#200315=CARTESIAN_POINT('Ctrl Pts',(-17.8597039230959,21.1390384546708,
13.5412535608802));
#200316=CARTESIAN_POINT('Ctrl Pts',(-17.8541742843991,21.1365213895884,
13.5416157861537));
#200317=CARTESIAN_POINT('Ctrl Pts',(-17.8427963618096,21.1312829695245,
13.5423642814023));
#200318=CARTESIAN_POINT('Ctrl Pts',(-17.8369495330777,21.1285586213036,
13.5427506517684));
#200319=CARTESIAN_POINT('Ctrl Pts',(-17.8233714229143,21.122156167156,13.5436520162441));
#200320=CARTESIAN_POINT('Ctrl Pts',(-17.8156498622229,21.1184578165047,
13.5441677086104));
#200321=CARTESIAN_POINT('Ctrl Pts',(-17.7910029068766,21.1064684618992,
13.5458238780106));
#200322=CARTESIAN_POINT('Ctrl Pts',(-17.7741660771847,21.0979984134206,
13.5469705797089));
#200323=CARTESIAN_POINT('Ctrl Pts',(-17.6906066949246,21.0545548102838,
13.5527402077935));
#200324=CARTESIAN_POINT('Ctrl Pts',(-17.6256781307248,21.0162657399933,
13.5574795258667));
#200325=CARTESIAN_POINT('Ctrl Pts',(-17.4719916056283,20.9142148557906,
13.56933492155));
#200326=CARTESIAN_POINT('Ctrl Pts',(-17.3858631201174,20.8468879893223,
13.5765508349481));
#200327=CARTESIAN_POINT('Ctrl Pts',(-17.2948305625363,20.7636371976547,
13.5847000357109));
#200328=CARTESIAN_POINT('Ctrl Pts',(-17.2844408245612,20.7539417154176,
13.5856382940039));
#200329=CARTESIAN_POINT('Ctrl Pts',(-17.1984073358917,20.6720210528694,
13.5934725087206));
#200330=CARTESIAN_POINT('Ctrl Pts',(-17.1281043658413,20.5943769405515,
13.6003057273877));
#200331=CARTESIAN_POINT('Ctrl Pts',(-17.0578711603,20.5042033629754,13.6073674632274));
#200332=CARTESIAN_POINT('Ctrl Pts',(-17.0519715232657,20.4965205315062,
13.6079626175343));
#200333=CARTESIAN_POINT('Ctrl Pts',(-17.0433374320107,20.4851155385267,
13.6088362114199));
#200334=CARTESIAN_POINT('Ctrl Pts',(-17.040562187945,20.4814246148239,13.6091174113764));
#200335=CARTESIAN_POINT('Ctrl Pts',(-17.0356595919814,20.4748598191969,
13.6096148357817));
#200336=CARTESIAN_POINT('Ctrl Pts',(-17.0335274236828,20.4719896121543,
13.6098313945607));
#200337=CARTESIAN_POINT('Ctrl Pts',(-17.028974171406,20.4658277251645,13.6102943326234));
#200338=CARTESIAN_POINT('Ctrl Pts',(-17.0265553493484,20.462534442844,13.6105405553369));
#200339=CARTESIAN_POINT('Ctrl Pts',(-17.0199405679013,20.4534733943254,
13.6112147826908));
#200340=CARTESIAN_POINT('Ctrl Pts',(-17.0157641537798,20.4476913327236,
13.6116414531712));
#200341=CARTESIAN_POINT('Ctrl Pts',(-16.9936027444247,20.4166808511105,
13.6139114216754));
#200342=CARTESIAN_POINT('Ctrl Pts',(-16.976142973047,20.3910795833401,13.6157208529884));
#200343=CARTESIAN_POINT('Ctrl Pts',(-16.8700919879331,20.2279971119139,
13.6269095658083));
#200344=CARTESIAN_POINT('Ctrl Pts',(-16.7971117252015,20.08100710477,13.6355534560693));
#200345=CARTESIAN_POINT('Ctrl Pts',(-16.7019663340167,19.8162959932826,
13.6509482649424));
#200346=CARTESIAN_POINT('Ctrl Pts',(-16.6714648710796,19.702413833633,13.6575165039292));
#200347=CARTESIAN_POINT('Ctrl Pts',(-16.6480480843424,19.5725219542311,
13.665248561539));
#200348=CARTESIAN_POINT('Ctrl Pts',(-16.6456535449103,19.558422777603,13.6660907125647));
#200349=CARTESIAN_POINT('Ctrl Pts',(-16.6420704654663,19.5359482403451,
13.6674381292322));
#200350=CARTESIAN_POINT('Ctrl Pts',(-16.6407889321607,19.5275879951391,
13.6679404478851));
#200351=CARTESIAN_POINT('Ctrl Pts',(-16.6386173999257,19.5128318352392,
13.6688290793997));
#200352=CARTESIAN_POINT('Ctrl Pts',(-16.6377064969351,19.5064390716212,
13.6692147251802));
#200353=CARTESIAN_POINT('Ctrl Pts',(-16.6358832057738,19.4932100011355,
13.6700141927525));
#200354=CARTESIAN_POINT('Ctrl Pts',(-16.634974950105,19.4863732106015,13.6704281403574));
#200355=CARTESIAN_POINT('Ctrl Pts',(-16.6327298117594,19.4688164098904,
13.6714932152976));
#200356=CARTESIAN_POINT('Ctrl Pts',(-16.6314415602274,19.4580904809252,
13.6721458697233));
#200357=CARTESIAN_POINT('Ctrl Pts',(-16.626410871443,19.4133130466284,13.6748790093008));
#200358=CARTESIAN_POINT('Ctrl Pts',(-16.6234133010094,19.3791846434934,
13.6769827635283));
#200359=CARTESIAN_POINT('Ctrl Pts',(-16.6177639888532,19.2901129386877,
13.6825301532353));
#200360=CARTESIAN_POINT('Ctrl Pts',(-16.616423234907,19.2351151293326,13.68601205213));
#200361=CARTESIAN_POINT('Ctrl Pts',(-16.6188189115814,19.0708366898491,
13.6965716227702));
#200362=CARTESIAN_POINT('Ctrl Pts',(-16.6288749874301,18.9618373954453,
13.7037977181733));
#200363=CARTESIAN_POINT('Ctrl Pts',(-16.6538425841158,18.8158536983178,
13.7135812115727));
#200364=CARTESIAN_POINT('Ctrl Pts',(-16.6614368350322,18.7777823795572,
13.7161412133366));
#200365=CARTESIAN_POINT('Ctrl Pts',(-16.6764912378106,18.7118221375845,
13.7205728943199));
#200366=CARTESIAN_POINT('Ctrl Pts',(-16.6834830384574,18.6838367104809,
13.7224519500333));
#200367=CARTESIAN_POINT('Ctrl Pts',(-16.7047152055288,18.6056807940748,
13.7276820630421));
#200368=CARTESIAN_POINT('Ctrl Pts',(-16.7202415782594,18.5558770246373,
13.7309945093287));
#200369=CARTESIAN_POINT('Ctrl Pts',(-16.7404765866114,18.4985194529803,
13.7347461132353));
#200370=CARTESIAN_POINT('Ctrl Pts',(-16.743410493025,18.4903630940372,13.7352780729219));
#200371=CARTESIAN_POINT('Ctrl Pts',(-16.7479339129004,18.4780262654958,
13.7360801170336));
#200372=CARTESIAN_POINT('Ctrl Pts',(-16.7494866725608,18.4738325482864,
13.736352308023));
#200373=CARTESIAN_POINT('Ctrl Pts',(-16.7523005262892,18.466306175514,13.7368399498039));
#200374=CARTESIAN_POINT('Ctrl Pts',(-16.7535567499692,18.462971771712,13.737055684844));
#200375=CARTESIAN_POINT('Ctrl Pts',(-16.7563079875154,18.4557246546391,
13.7375239044768));
#200376=CARTESIAN_POINT('Ctrl Pts',(-16.7578061915396,18.4518132142513,
13.7377761949221));
#200377=CARTESIAN_POINT('Ctrl Pts',(-16.7620557074149,18.4408165962108,
13.7384843727062));
#200378=CARTESIAN_POINT('Ctrl Pts',(-16.7648336130568,18.4337416690485,
13.7389386937051));
#200379=CARTESIAN_POINT('Ctrl Pts',(-16.7818510285622,18.3910776088956,
13.7416713945337));
#200380=CARTESIAN_POINT('Ctrl Pts',(-16.7970178564852,18.3558632130923,
13.7438974389364));
#200381=CARTESIAN_POINT('Ctrl Pts',(-16.8505630681125,18.2402877311501,
13.7511661148448));
#200382=CARTESIAN_POINT('Ctrl Pts',(-16.8930552414599,18.1619328442462,
13.7560350381166));
#200383=CARTESIAN_POINT('Ctrl Pts',(-17.0320404974686,17.9402470947443,
13.7702655157221));
#200384=CARTESIAN_POINT('Ctrl Pts',(-17.1412483627253,17.8057902296815,
13.7795583728622));
#200385=CARTESIAN_POINT('Ctrl Pts',(-17.2822664521819,17.6699949292943,
13.7909320811994));
#200386=CARTESIAN_POINT('Ctrl Pts',(-17.2992356712801,17.6541833183271,
13.7922906819857));
#200387=CARTESIAN_POINT('Ctrl Pts',(-17.3235756328385,17.6322397680457,
13.7942272443052));
#200388=CARTESIAN_POINT('Ctrl Pts',(-17.3307338664818,17.6258738474745,
13.7947953253153));
#200389=CARTESIAN_POINT('Ctrl Pts',(-17.3424250660992,17.6156179520643,
13.7957209251555));
#200390=CARTESIAN_POINT('Ctrl Pts',(-17.3469317748016,17.6116981482359,
13.7960771956445));
#200391=CARTESIAN_POINT('Ctrl Pts',(-17.3563921587688,17.6035398483496,
13.7968240031664));
#200392=CARTESIAN_POINT('Ctrl Pts',(-17.3613489390923,17.5993050639532,
13.797214687981));
#200393=CARTESIAN_POINT('Ctrl Pts',(-17.3731730123563,17.5892973776681,
13.7981452520512));
#200394=CARTESIAN_POINT('Ctrl Pts',(-17.3800575552127,17.583545134909,13.7986859688505));
#200395=CARTESIAN_POINT('Ctrl Pts',(-17.4033060344955,17.5643699500663,
13.800508383325));
#200396=CARTESIAN_POINT('Ctrl Pts',(-17.4198342468994,17.5511490206937,
13.8017981910926));
#200397=CARTESIAN_POINT('Ctrl Pts',(-17.5837507900191,17.4240151353829,
13.8145374047678));
#200398=CARTESIAN_POINT('Ctrl Pts',(-17.7453418021745,17.3297996082595,
13.8267959554362));
#200399=CARTESIAN_POINT('Ctrl Pts',(-17.985069458636,17.2295317459592,13.8439543901627));
#200400=CARTESIAN_POINT('Ctrl Pts',(-18.0544568764968,17.2046760562962,
13.8487976709831));
#200401=CARTESIAN_POINT('Ctrl Pts',(-18.165646234112,17.1712784552811,13.8562423375453));
#200402=CARTESIAN_POINT('Ctrl Pts',(-18.2066515294104,17.1602942353662,
13.8589218089182));
#200403=CARTESIAN_POINT('Ctrl Pts',(-18.2552234349893,17.1488366557899,
13.8619971148717));
#200404=CARTESIAN_POINT('Ctrl Pts',(-18.2624936686226,17.1471622058291,
13.8624548502572));
#200405=CARTESIAN_POINT('Ctrl Pts',(-18.2742693389211,17.1445155552961,
13.8631919173556));
#200406=CARTESIAN_POINT('Ctrl Pts',(-18.2787692913511,17.1435195904749,
13.8634725594934));
#200407=CARTESIAN_POINT('Ctrl Pts',(-18.2867651039416,17.1417772654529,
13.8639693679803));
#200408=CARTESIAN_POINT('Ctrl Pts',(-18.2902596332116,17.1410250569211,
13.8641858655702));
#200409=CARTESIAN_POINT('Ctrl Pts',(-18.2977584812327,17.1394307686739,
13.8646490839349));
#200410=CARTESIAN_POINT('Ctrl Pts',(-18.3017633297011,17.1385914484894,
13.864895645988));
#200411=CARTESIAN_POINT('Ctrl Pts',(-18.3127811107521,17.1363157129291,
13.8655717605959));
#200412=CARTESIAN_POINT('Ctrl Pts',(-18.3197990095529,17.1349032328616,
13.8659999665215));
#200413=CARTESIAN_POINT('Ctrl Pts',(-18.3575837602118,17.1274975833521,
13.8682929269956));
#200414=CARTESIAN_POINT('Ctrl Pts',(-18.3884754364149,17.1221523469643,
13.8701229969894));
#200415=CARTESIAN_POINT('Ctrl Pts',(-18.5813618835597,17.0931734967987,
13.8813369939068));
#200416=CARTESIAN_POINT('Ctrl Pts',(-18.7455393716564,17.0877085388961,
13.8899877300423));
#200417=CARTESIAN_POINT('Ctrl Pts',(-19.0254742134598,17.1108912785544,
13.9053635781708));
#200418=CARTESIAN_POINT('Ctrl Pts',(-19.141208036955,17.1302332706494,13.9119026743156));
#200419=CARTESIAN_POINT('Ctrl Pts',(-19.2685946818074,17.1625611192414,
13.9196019305026));
#200420=CARTESIAN_POINT('Ctrl Pts',(-19.2824133907115,17.1662173562977,
13.9204436838361));
#200421=CARTESIAN_POINT('Ctrl Pts',(-19.3043460798495,17.1722587579597,
13.9217905830302));
#200422=CARTESIAN_POINT('Ctrl Pts',(-19.3124847735985,17.1745531270505,
13.922292785483));
#200423=CARTESIAN_POINT('Ctrl Pts',(-19.3268136050104,17.1786853779578,
13.9231812816236));
#200424=CARTESIAN_POINT('Ctrl Pts',(-19.3330095236222,17.1805029469522,
13.9235669088817));
#200425=CARTESIAN_POINT('Ctrl Pts',(-19.3458068012147,17.1843206923529,
13.9243664069672));
#200426=CARTESIAN_POINT('Ctrl Pts',(-19.3524068863343,17.1863248410572,
13.9247804039474));
#200427=CARTESIAN_POINT('Ctrl Pts',(-19.3693219965263,17.1915516235456,
13.9258457510259));
#200428=CARTESIAN_POINT('Ctrl Pts',(-19.3796222597459,17.194821020997,13.9264986297217));
#200429=CARTESIAN_POINT('Ctrl Pts',(-19.4218508079554,17.2085815278659,
13.9291926508531));
#200430=CARTESIAN_POINT('Ctrl Pts',(-19.4535506985597,17.2197528881829,
13.9312560907756));
#200431=CARTESIAN_POINT('Ctrl Pts',(-19.5353266317394,17.2507792325233,
13.9366900412467));
#200432=CARTESIAN_POINT('Ctrl Pts',(-19.5849322295837,17.2717982573215,
13.9400972212999));
#200433=CARTESIAN_POINT('Ctrl Pts',(-19.7592183513054,17.3536227888732,
13.9524604745935));
#200434=CARTESIAN_POINT('Ctrl Pts',(-19.8786546037046,17.4247518687682,
13.9617005146233));
#200435=CARTESIAN_POINT('Ctrl Pts',(-20.0634095985323,17.5609643854179,
13.9767909036667));
#200436=CARTESIAN_POINT('Ctrl Pts',(-20.133015894145,17.6195522910692,13.982688180589));
#200437=CARTESIAN_POINT('Ctrl Pts',(-20.2056224655865,17.6891229876435,
13.9889007028638));
#200438=CARTESIAN_POINT('Ctrl Pts',(-20.2125519416844,17.6958543021151,
13.9894942389475));
#200439=CARTESIAN_POINT('Ctrl Pts',(-20.2227218545077,17.7058696011461,
13.990365919543));
#200440=CARTESIAN_POINT('Ctrl Pts',(-20.2259979113813,17.7091170115463,
13.9906468073772));
#200441=CARTESIAN_POINT('Ctrl Pts',(-20.2317940786145,17.7149001776599,
13.9911438870016));
#200442=CARTESIAN_POINT('Ctrl Pts',(-20.2343184032069,17.7174316319589,
13.9913604113936));
#200443=CARTESIAN_POINT('Ctrl Pts',(-20.2397164879855,17.7228724584363,
13.991823505609));
#200444=CARTESIAN_POINT('Ctrl Pts',(-20.242588226541,17.7257837579852,13.992069917661));
#200445=CARTESIAN_POINT('Ctrl Pts',(-20.2484651363593,17.7317762592988,
13.9925743398287));
#200446=CARTESIAN_POINT('Ctrl Pts',(-20.251469385212,17.7348583435255,13.9928322786039));
#200447=CARTESIAN_POINT('Ctrl Pts',(-20.2652668859293,17.7490999516008,
13.9940173986629));
#200448=CARTESIAN_POINT('Ctrl Pts',(-20.2759468995372,17.7603691654818,
13.994936146573));
#200449=CARTESIAN_POINT('Ctrl Pts',(-20.3410501612763,17.8305955550524,
14.0005530642606));
#200450=CARTESIAN_POINT('Ctrl Pts',(-20.3922148590281,17.8924959727615,
14.0050404365917));
#200451=CARTESIAN_POINT('Ctrl Pts',(-20.4809417866774,18.0132014549934,
14.0132761495103));
#200452=CARTESIAN_POINT('Ctrl Pts',(-20.5193513602725,18.071242185948,14.0170383228645));
#200453=CARTESIAN_POINT('Ctrl Pts',(-20.6313102356392,18.2600122713974,
14.0289664352486));
#200454=CARTESIAN_POINT('Ctrl Pts',(-20.6938625840409,18.396694031845,14.0371981702937));
#200455=CARTESIAN_POINT('Ctrl Pts',(-20.745951993975,18.5522596433864,14.0468106106721));
#200456=CARTESIAN_POINT('Ctrl Pts',(-20.7503149288445,18.5657374358616,
14.0476449383686));
#200457=CARTESIAN_POINT('Ctrl Pts',(-20.7570544842117,18.5872929930894,
14.0489821722094));
#200458=CARTESIAN_POINT('Ctrl Pts',(-20.7595187957101,18.5953430487196,
14.049482201439));
#200459=CARTESIAN_POINT('Ctrl Pts',(-20.7637864754445,18.6095870973499,
14.0503681693453));
#200460=CARTESIAN_POINT('Ctrl Pts',(-20.7656096811759,18.6157750699929,
14.0507534537642));
#200461=CARTESIAN_POINT('Ctrl Pts',(-20.7693280079652,18.6286112216265,
14.0515535403252));
#200462=CARTESIAN_POINT('Ctrl Pts',(-20.7712189024992,18.6352605357287,
14.0519684750335));
#200463=CARTESIAN_POINT('Ctrl Pts',(-20.7760008794889,18.652394861015,14.0530389870521));
#200464=CARTESIAN_POINT('Ctrl Pts',(-20.7788437624975,18.6628930093539,
14.0536961216643));
#200465=CARTESIAN_POINT('Ctrl Pts',(-20.7848190523309,18.6856521613353,
14.0551235603184));
#200466=CARTESIAN_POINT('Ctrl Pts',(-20.7879226552397,18.6979202280657,
14.0558947687061));
#200467=CARTESIAN_POINT('Ctrl Pts',(-20.79663370116,18.7336998467524,14.0581493586585));
#200468=CARTESIAN_POINT('Ctrl Pts',(-20.8019485569284,18.7572799187343,
14.0596419606873));
#200469=CARTESIAN_POINT('Ctrl Pts',(-20.8363441724377,18.9230662790745,
14.0701853687219));
#200470=CARTESIAN_POINT('Ctrl Pts',(-20.8511300495927,19.0678165918601,
14.0796831108336));
#200471=CARTESIAN_POINT('Ctrl Pts',(-20.8509991383142,19.2129100724755,
14.0892705377863));
#200472=CARTESIAN_POINT('Ctrl Pts',(-20.8509991377702,19.2129106753478,
14.0892705776226));
#200473=CARTESIAN_POINT('Ctrl Pts',(-20.8508884782116,19.3355197780962,
14.0973722912252));
#200474=CARTESIAN_POINT('Ctrl Pts',(-20.840126423568,19.4579019518155,14.1054939843093));
#200475=CARTESIAN_POINT('Ctrl Pts',(-20.8166444881502,19.5910510982751,
14.1139586039406));
#200476=CARTESIAN_POINT('Ctrl Pts',(-20.814351877406,19.6034066563032,14.1147403450995));
#200477=CARTESIAN_POINT('Ctrl Pts',(-20.8106712450187,19.6223030872299,
14.1159294515346));
#200478=CARTESIAN_POINT('Ctrl Pts',(-20.8093620687928,19.6288587985602,
14.116340787568));
#200479=CARTESIAN_POINT('Ctrl Pts',(-20.8071513247562,19.6396623843232,
14.1170165517433));
#200480=CARTESIAN_POINT('Ctrl Pts',(-20.8062677127861,19.6439138278879,
14.1172819409962));
#200481=CARTESIAN_POINT('Ctrl Pts',(-20.8045210246822,19.6521900148307,
14.1177974780946));
#200482=CARTESIAN_POINT('Ctrl Pts',(-20.803659279343,19.6562150165181,14.1180476988373));
#200483=CARTESIAN_POINT('Ctrl Pts',(-20.8020280139603,19.6637271643379,
14.1185137302678));
#200484=CARTESIAN_POINT('Ctrl Pts',(-20.8012614185717,19.6672148390563,
14.1187296988306));
#200485=CARTESIAN_POINT('Ctrl Pts',(-20.7994932703674,19.6751631714775,
14.1192209982101));
#200486=CARTESIAN_POINT('Ctrl Pts',(-20.7984860931349,19.6796225259647,
14.1194960031171));
#200487=CARTESIAN_POINT('Ctrl Pts',(-20.7953527020391,19.6932896856474,
14.1203369943829));
#200488=CARTESIAN_POINT('Ctrl Pts',(-20.7931792402637,19.702486690609,14.1209003387533));
#200489=CARTESIAN_POINT('Ctrl Pts',(-20.7723521707152,19.7880524400293,
14.1261200192409));
#200490=CARTESIAN_POINT('Ctrl Pts',(-20.749526058459,19.8633154573807,14.1305523841898));
#200491=CARTESIAN_POINT('Ctrl Pts',(-20.7225805809329,19.9371103725581,
14.1348941200942));
#200492=CARTESIAN_POINT('Origin',(-18.734,19.211,0.));
#200493=CARTESIAN_POINT('',(-20.7225806064499,19.9371103026755,15.1555945416419));
#200494=CARTESIAN_POINT('',(-20.7225805830531,19.9371103667517,14.9318515409431));
#200495=CARTESIAN_POINT('',(-20.7225806064498,19.9371103026755,0.));
#200496=CARTESIAN_POINT('',(-20.8523540121835,19.2127405753659,15.110942953294));
#200497=CARTESIAN_POINT('Ctrl Pts',(-20.8509992748742,19.2127521935257,
15.1109437209775));
#200498=CARTESIAN_POINT('Ctrl Pts',(-20.8509006165464,19.3319511321298,
15.1181312937192));
#200499=CARTESIAN_POINT('Ctrl Pts',(-20.8407310772906,19.4507453566806,
15.1253188664609));
#200500=CARTESIAN_POINT('Ctrl Pts',(-20.8207141748805,19.5678094061999,
15.1325064392026));
#200501=CARTESIAN_POINT('Ctrl Pts',(-20.8084963315169,19.6392625307264,
15.1368935634501));
#200502=CARTESIAN_POINT('Ctrl Pts',(-20.7925803619098,19.7102268266174,
15.1412806876976));
#200503=CARTESIAN_POINT('Ctrl Pts',(-20.7730188005824,19.7802901991706,
15.145667811945));
#200504=CARTESIAN_POINT('Ctrl Pts',(-20.75826484326,19.8331342432225,15.148976721844));
#200505=CARTESIAN_POINT('Ctrl Pts',(-20.7414381049983,19.8854657305472,
15.152285631743));
#200506=CARTESIAN_POINT('Ctrl Pts',(-20.7225806064499,19.9371103026755,
15.1555945416419));
#200507=CARTESIAN_POINT('Ctrl Pts',(-20.7249099185723,19.937940853899,14.355439970105));
#200508=CARTESIAN_POINT('Ctrl Pts',(-20.6989346035943,20.0108543135692,
14.360110513108));
#200509=CARTESIAN_POINT('Ctrl Pts',(-20.3954319215272,20.7297352208536,
14.4071729916714));
#200510=CARTESIAN_POINT('Ctrl Pts',(-19.0148744787979,21.6984565315259,
14.4966274057954));
#200511=CARTESIAN_POINT('Ctrl Pts',(-16.7944747336859,20.7935840294885,
14.6238032124768));
#200512=CARTESIAN_POINT('Ctrl Pts',(-16.3534690399024,18.4367889066407,
14.7509790191583));
#200513=CARTESIAN_POINT('Ctrl Pts',(-18.0964527495933,16.7902844089888,
14.8781548258396));
#200514=CARTESIAN_POINT('Ctrl Pts',(-20.2927766449214,17.3321745234098,
14.9981428038849));
#200515=CARTESIAN_POINT('Ctrl Pts',(-20.8471440588156,18.6285361211804,
15.0757388463697));
#200516=CARTESIAN_POINT('Ctrl Pts',(-20.8523540121835,19.2127405753659,
15.110942953294));
#200517=CARTESIAN_POINT('Ctrl Pts',(-20.7225805809329,19.9371103725581,
14.1348941200942));
#200518=CARTESIAN_POINT('Ctrl Pts',(-20.7075027445907,19.9784036713261,
14.1373236180813));
#200519=CARTESIAN_POINT('Ctrl Pts',(-20.6911350749698,20.0192372971913,
14.1397245483283));
#200520=CARTESIAN_POINT('Ctrl Pts',(-20.6449226516951,20.1248631733796,
14.1459967998668));
#200521=CARTESIAN_POINT('Ctrl Pts',(-20.6130668885677,20.1886905292902,
14.1498508365716));
#200522=CARTESIAN_POINT('Ctrl Pts',(-20.5342698885964,20.3284360931426,
14.158640741542));
#200523=CARTESIAN_POINT('Ctrl Pts',(-20.4856308923035,20.4032340607066,
14.1635990977973));
#200524=CARTESIAN_POINT('Ctrl Pts',(-20.4120570099747,20.5021150089675,
14.1706900328253));
#200525=CARTESIAN_POINT('Ctrl Pts',(-20.39103012142,20.5289925183535,14.172676241559));
#200526=CARTESIAN_POINT('Ctrl Pts',(-20.3624522619252,20.5637566990417,
14.1753300352325));
#200527=CARTESIAN_POINT('Ctrl Pts',(-20.3554761641233,20.5721107591439,
14.1759744171542));
#200528=CARTESIAN_POINT('Ctrl Pts',(-20.3439632380515,20.5856836669195,
14.177032489082));
#200529=CARTESIAN_POINT('Ctrl Pts',(-20.3394646543371,20.5909348005986,
14.1774446068526));
#200530=CARTESIAN_POINT('Ctrl Pts',(-20.3307199602477,20.6010417172682,
14.1782432344864));
#200531=CARTESIAN_POINT('Ctrl Pts',(-20.326477218989,20.6059003235973,14.1786296020724));
#200532=CARTESIAN_POINT('Ctrl Pts',(-20.3166485363715,20.6170524245627,
14.1795221554944));
#200533=CARTESIAN_POINT('Ctrl Pts',(-20.3110471704809,20.6233321242477,
14.1800289844274));
#200534=CARTESIAN_POINT('Ctrl Pts',(-20.2959249753151,20.6400835076497,
14.1813924909934));
#200535=CARTESIAN_POINT('Ctrl Pts',(-20.2863364528878,20.6504932518482,
14.1822520255119));
#200536=CARTESIAN_POINT('Ctrl Pts',(-20.2021775981613,20.7400412337915,
14.1897542468199));
#200537=CARTESIAN_POINT('Ctrl Pts',(-20.1217285188347,20.8134093595933,
14.196656521211));
#200538=CARTESIAN_POINT('Ctrl Pts',(-19.9589779544846,20.9403532531287,
14.2100961836297));
#200539=CARTESIAN_POINT('Ctrl Pts',(-19.8778787207691,20.9950329876922,
14.2165813580757));
#200540=CARTESIAN_POINT('Ctrl Pts',(-19.7310563154312,21.0798862323185,
14.2277585212487));
#200541=CARTESIAN_POINT('Ctrl Pts',(-19.6670177360556,21.1126667382505,
14.2324626464547));
#200542=CARTESIAN_POINT('Ctrl Pts',(-19.5707240266837,21.1559203325036,
14.2391778324342));
#200543=CARTESIAN_POINT('Ctrl Pts',(-19.5396899638316,21.1689801262702,
14.2412894979581));
#200544=CARTESIAN_POINT('Ctrl Pts',(-19.5015751173138,21.1839598365988,
14.2438083954485));
#200545=CARTESIAN_POINT('Ctrl Pts',(-19.4947807280694,21.1865897258538,
14.2442545711192));
#200546=CARTESIAN_POINT('Ctrl Pts',(-19.4840926108851,21.190663435538,14.2449518292703));
#200547=CARTESIAN_POINT('Ctrl Pts',(-19.4802080551625,21.1921309350987,
14.2452042927434));
#200548=CARTESIAN_POINT('Ctrl Pts',(-19.4729790589859,21.1948376119825,
14.2456723144294));
#200549=CARTESIAN_POINT('Ctrl Pts',(-19.4696358374338,21.1960797553975,
14.2458880439109));
#200550=CARTESIAN_POINT('Ctrl Pts',(-19.4620487015655,21.1988768865442,
14.2463760091694));
#200551=CARTESIAN_POINT('Ctrl Pts',(-19.457802947611,21.2004267319526,14.2466479365073));
#200552=CARTESIAN_POINT('Ctrl Pts',(-19.445190966769,21.2049848170869,14.2474524144538));
#200553=CARTESIAN_POINT('Ctrl Pts',(-19.4368105974676,21.2079540085681,
14.2479826988741));
#200554=CARTESIAN_POINT('Ctrl Pts',(-19.3737718093276,21.2298428602992,
14.2519413590458));
#200555=CARTESIAN_POINT('Ctrl Pts',(-19.3183720860012,21.2465699437743,
14.2552503475475));
#200556=CARTESIAN_POINT('Ctrl Pts',(-19.1043072086437,21.3017412218326,
14.2676373541398));
#200557=CARTESIAN_POINT('Ctrl Pts',(-18.9420769950573,21.324063329741,14.2762437750213));
#200558=CARTESIAN_POINT('Ctrl Pts',(-18.7188478806076,21.3287973145088,
14.2886115840558));
#200559=CARTESIAN_POINT('Ctrl Pts',(-18.6587878699798,21.3275153878792,
14.2919854993993));
#200560=CARTESIAN_POINT('Ctrl Pts',(-18.5747286589263,21.3221387123029,
14.2968224145711));
#200561=CARTESIAN_POINT('Ctrl Pts',(-18.5506197109285,21.3201812688754,
14.2982228471611));
#200562=CARTESIAN_POINT('Ctrl Pts',(-18.5085712708542,21.316040917951,14.3006913188793));
#200563=CARTESIAN_POINT('Ctrl Pts',(-18.4906161078813,21.3140405676679,
14.301753686834));
#200564=CARTESIAN_POINT('Ctrl Pts',(-18.4642184900994,21.3107570809678,
14.3033286556341));
#200565=CARTESIAN_POINT('Ctrl Pts',(-18.4557543798612,21.3096522422203,
14.3038356368359));
#200566=CARTESIAN_POINT('Ctrl Pts',(-18.4409102064075,21.3076232207399,
14.3047283447093));
#200567=CARTESIAN_POINT('Ctrl Pts',(-18.4345272129133,21.3067210227579,
14.30511337166));
#200568=CARTESIAN_POINT('Ctrl Pts',(-18.4221291229341,21.3049108293485,
14.3058635331603));
#200569=CARTESIAN_POINT('Ctrl Pts',(-18.4161136177958,21.3040060324884,
14.3062285627946));
#200570=CARTESIAN_POINT('Ctrl Pts',(-18.4017234817992,21.3017781326947,
14.3071043381384));
#200571=CARTESIAN_POINT('Ctrl Pts',(-18.3933527848819,21.3004306296843,
14.307615853762));
#200572=CARTESIAN_POINT('Ctrl Pts',(-18.3630621143995,21.2953676195601,
14.309474522269));
#200573=CARTESIAN_POINT('Ctrl Pts',(-18.3411935150339,21.2913572516898,
14.310830997205));
#200574=CARTESIAN_POINT('Ctrl Pts',(-18.1386282032922,21.2509020932711,
14.3235359568818));
#200575=CARTESIAN_POINT('Ctrl Pts',(-17.9633851786215,21.1913519550015,
14.3356714120186));
#200576=CARTESIAN_POINT('Ctrl Pts',(-17.7254648935146,21.0740901273226,
14.3531857352959));
#200577=CARTESIAN_POINT('Ctrl Pts',(-17.6549310632739,21.0341455939937,
14.3585088996915));
#200578=CARTESIAN_POINT('Ctrl Pts',(-17.5563846289528,20.970609467035,14.3659848135715));
#200579=CARTESIAN_POINT('Ctrl Pts',(-17.5264210921241,20.9501828496055,
14.368262971875));
#200580=CARTESIAN_POINT('Ctrl Pts',(-17.4909249822137,20.9246246522119,
14.3709540367914));
#200581=CARTESIAN_POINT('Ctrl Pts',(-17.4848779903975,20.9202217987955,
14.3714121961819));
#200582=CARTESIAN_POINT('Ctrl Pts',(-17.4755025499349,20.9133191512315,
14.3721219370661));
#200583=CARTESIAN_POINT('Ctrl Pts',(-17.4721579929903,20.910841485111,14.3723750066527));
#200584=CARTESIAN_POINT('Ctrl Pts',(-17.465961969051,20.9062230724059,14.3728435773018));
#200585=CARTESIAN_POINT('Ctrl Pts',(-17.463108629678,20.9040850062153,14.3730592532255));
#200586=CARTESIAN_POINT('Ctrl Pts',(-17.4566612144526,20.8992283418441,
14.3735463677906));
#200587=CARTESIAN_POINT('Ctrl Pts',(-17.4530704185527,20.8965054777441,
14.3738175025004));
#200588=CARTESIAN_POINT('Ctrl Pts',(-17.4422376509934,20.888236488411,14.3746350825371));
#200589=CARTESIAN_POINT('Ctrl Pts',(-17.4350226952681,20.8826549204064,
14.3751790954352));
#200590=CARTESIAN_POINT('Ctrl Pts',(-17.3795538997159,20.839167680719,14.379359391647));
#200591=CARTESIAN_POINT('Ctrl Pts',(-17.3329278455319,20.7992230759704,
14.3828612289333));
#200592=CARTESIAN_POINT('Ctrl Pts',(-17.1808303155901,20.6570015085998,
14.3944981721722));
#200593=CARTESIAN_POINT('Ctrl Pts',(-17.0842857608965,20.5458048286567,
14.4022854888115));
#200594=CARTESIAN_POINT('Ctrl Pts',(-16.946810279657,20.3495280655668,14.4154839112159));
#200595=CARTESIAN_POINT('Ctrl Pts',(-16.8986517639734,20.2701445724771,
14.4206924526458));
#200596=CARTESIAN_POINT('Ctrl Pts',(-16.8461314902584,20.1691678592443,
14.4273222647719));
#200597=CARTESIAN_POINT('Ctrl Pts',(-16.8366866789988,20.1503270310562,
14.4285591608391));
#200598=CARTESIAN_POINT('Ctrl Pts',(-16.8236313879887,20.1232833866047,
14.4303357088599));
#200599=CARTESIAN_POINT('Ctrl Pts',(-16.8197890746599,20.1151934200088,
14.4308672946605));
#200600=CARTESIAN_POINT('Ctrl Pts',(-16.8132398763448,20.1011752719942,
14.4317887620705));
#200601=CARTESIAN_POINT('Ctrl Pts',(-16.8105087979129,20.0952584811709,
14.4321778010639));
#200602=CARTESIAN_POINT('Ctrl Pts',(-16.8053256295102,20.0838916813101,
14.4329254282378));
#200603=CARTESIAN_POINT('Ctrl Pts',(-16.8028692096263,20.0784437065406,
14.4332838626625));
#200604=CARTESIAN_POINT('Ctrl Pts',(-16.7965281041514,20.0642196452384,
14.4342200070783));
#200605=CARTESIAN_POINT('Ctrl Pts',(-16.7926800043324,20.0554274864664,
14.4347989638389));
#200606=CARTESIAN_POINT('Ctrl Pts',(-16.7796943185482,20.0251997776535,
14.436790666187));
#200607=CARTESIAN_POINT('Ctrl Pts',(-16.7708511825201,20.0036402884189,
14.43821335448));
#200608=CARTESIAN_POINT('Ctrl Pts',(-16.7001112797976,19.8227270908541,
14.4501735258314));
#200609=CARTESIAN_POINT('Ctrl Pts',(-16.6573818896966,19.6565882069872,
14.461374321672));
#200610=CARTESIAN_POINT('Ctrl Pts',(-16.6233195846727,19.3977037016305,
14.4786292814234));
#200611=CARTESIAN_POINT('Ctrl Pts',(-16.617279810624,19.3075801299548,14.4845839137008));
#200612=CARTESIAN_POINT('Ctrl Pts',(-16.6168937955224,19.1787164502282,
14.492816935175));
#200613=CARTESIAN_POINT('Ctrl Pts',(-16.6178351962036,19.1400925501234,
14.4952478567591));
#200614=CARTESIAN_POINT('Ctrl Pts',(-16.6202270324269,19.0939066198248,
14.498094016606));
#200615=CARTESIAN_POINT('Ctrl Pts',(-16.6206620228555,19.0863018984478,
14.4985606726401));
#200616=CARTESIAN_POINT('Ctrl Pts',(-16.6214000360126,19.0745156949966,
14.4992806819838));
#200617=CARTESIAN_POINT('Ctrl Pts',(-16.6216744450782,19.0703325763396,
14.4995355922054));
#200618=CARTESIAN_POINT('Ctrl Pts',(-16.6222050645947,19.0625956694284,
14.5000058566502));
#200619=CARTESIAN_POINT('Ctrl Pts',(-16.6224578188473,19.0590417423849,
14.5002213965798));
#200620=CARTESIAN_POINT('Ctrl Pts',(-16.6230477153701,19.0510330994009,
14.5007060490312));
#200621=CARTESIAN_POINT('Ctrl Pts',(-16.6233899857452,19.0465788157189,
14.5009748708014));
#200622=CARTESIAN_POINT('Ctrl Pts',(-16.6244361134988,19.0335064084795,
14.5017617379335));
#200623=CARTESIAN_POINT('Ctrl Pts',(-16.6251786836259,19.0248913552421,
14.5022776619906));
#200624=CARTESIAN_POINT('Ctrl Pts',(-16.6307250371006,18.9648466096778,
14.5058565896829));
#200625=CARTESIAN_POINT('Ctrl Pts',(-16.6373573233712,18.9135987862299,
14.5088246083189));
#200626=CARTESIAN_POINT('Ctrl Pts',(-16.6494417926672,18.8411618435247,
14.5129605195427));
#200627=CARTESIAN_POINT('Ctrl Pts',(-16.6533563331053,18.8197390150789,
14.5141762236957));
#200628=CARTESIAN_POINT('Ctrl Pts',(-16.6665987112314,18.7531003226135,
14.5179446567348));
#200629=CARTESIAN_POINT('Ctrl Pts',(-16.677075593898,18.7081258244164,14.5204691137869));
#200630=CARTESIAN_POINT('Ctrl Pts',(-16.71729483546,18.5578937437471,14.52893643587));
#200631=CARTESIAN_POINT('Ctrl Pts',(-16.7537170532173,18.4546098425893,
14.5348247787239));
#200632=CARTESIAN_POINT('Ctrl Pts',(-16.8202492865064,18.3042006774433,
14.5439697023021));
#200633=CARTESIAN_POINT('Ctrl Pts',(-16.8445041512232,18.254688546192,14.5470775553507));
#200634=CARTESIAN_POINT('Ctrl Pts',(-16.8869471151252,18.1759821992873,
14.5522220740495));
#200635=CARTESIAN_POINT('Ctrl Pts',(-16.9039633383107,18.146184604005,14.5542193418497));
#200636=CARTESIAN_POINT('Ctrl Pts',(-16.9272822628123,18.1075613484377,
14.5568801673014));
#200637=CARTESIAN_POINT('Ctrl Pts',(-16.9329397966025,18.0983509192882,
14.5575201926022));
#200638=CARTESIAN_POINT('Ctrl Pts',(-16.9423229767659,18.0833342559912,
14.5585729226801));
#200639=CARTESIAN_POINT('Ctrl Pts',(-16.946006951958,18.0775021198882,14.5589840860392));
#200640=CARTESIAN_POINT('Ctrl Pts',(-16.9531942095638,18.0662461281677,
14.5597821569104));
#200641=CARTESIAN_POINT('Ctrl Pts',(-16.9566939348696,18.0608200837504,
14.5601689290155));
#200642=CARTESIAN_POINT('Ctrl Pts',(-16.9648334169415,18.0483263222915,
14.5610642963304));
#200643=CARTESIAN_POINT('Ctrl Pts',(-16.969490776313,18.0412702552592,14.5615735476171));
#200644=CARTESIAN_POINT('Ctrl Pts',(-16.9821331267667,18.0223639562508,
14.5629478146742));
#200645=CARTESIAN_POINT('Ctrl Pts',(-16.9901959324398,18.0105665181789,
14.5638157582371));
#200646=CARTESIAN_POINT('Ctrl Pts',(-17.0652574946945,17.9030891097816,
14.5718203439441));
#200647=CARTESIAN_POINT('Ctrl Pts',(-17.1399371142987,17.8130414299508,
14.5792585290705));
#200648=CARTESIAN_POINT('Ctrl Pts',(-17.3354199716359,17.6134713819786,
14.5975058499753));
#200649=CARTESIAN_POINT('Ctrl Pts',(-17.4621895610557,17.5108170568064,
14.6084547013722));
#200650=CARTESIAN_POINT('Ctrl Pts',(-17.6270395097253,17.4061745833797,
14.6208636871663));
#200651=CARTESIAN_POINT('Ctrl Pts',(-17.6550249474443,17.3893058929064,
14.6229115124145));
#200652=CARTESIAN_POINT('Ctrl Pts',(-17.6896861242341,17.3694924380092,
14.62536664193));
#200653=CARTESIAN_POINT('Ctrl Pts',(-17.695999451984,17.3659264410847,14.6258105989811));
#200654=CARTESIAN_POINT('Ctrl Pts',(-17.7059218470725,17.3603889601486,
14.6265031491889));
#200655=CARTESIAN_POINT('Ctrl Pts',(-17.7095184801269,17.3583954751621,
14.6267531183667));
#200656=CARTESIAN_POINT('Ctrl Pts',(-17.7162497645866,17.3546901621181,
14.6272189307998));
#200657=CARTESIAN_POINT('Ctrl Pts',(-17.7193829050965,17.3529758056304,
14.6274349304174));
#200658=CARTESIAN_POINT('Ctrl Pts',(-17.7265418266783,17.349082175748,14.62792662311));
#200659=CARTESIAN_POINT('Ctrl Pts',(-17.7305703391558,17.3469080301924,
14.628201988233));
#200660=CARTESIAN_POINT('Ctrl Pts',(-17.7429638644626,17.3402711939668,
14.62904517706));
#200661=CARTESIAN_POINT('Ctrl Pts',(-17.7513519619008,17.3358515449577,
14.629610338656));
#200662=CARTESIAN_POINT('Ctrl Pts',(-17.8671857826812,17.2758099794782,
14.6373430419722));
#200663=CARTESIAN_POINT('Ctrl Pts',(-17.9791940981658,17.2294339722747,
14.6439805394056));
#200664=CARTESIAN_POINT('Ctrl Pts',(-18.2651920541203,17.1388165594462,
14.6603064926629));
#200665=CARTESIAN_POINT('Ctrl Pts',(-18.4419635492511,17.1066158183815,
14.6699251819398));
#200666=CARTESIAN_POINT('Ctrl Pts',(-18.6421236112204,17.0958855459716,
14.6815961476636));
#200667=CARTESIAN_POINT('Ctrl Pts',(-18.6635892524944,17.0950622170958,
14.6828565027497));
#200668=CARTESIAN_POINT('Ctrl Pts',(-18.694085586048,17.0943570713107,14.6846608925073));
#200669=CARTESIAN_POINT('Ctrl Pts',(-18.7031091628754,17.0942061507193,
14.6851965060007));
#200670=CARTESIAN_POINT('Ctrl Pts',(-18.7186621421395,17.0940454940806,
14.68612274061));
#200671=CARTESIAN_POINT('Ctrl Pts',(-18.7251911802201,17.0940082585807,
14.6865124952718));
#200672=CARTESIAN_POINT('Ctrl Pts',(-18.7376819722161,17.0939948074014,
14.6872599541023));
#200673=CARTESIAN_POINT('Ctrl Pts',(-18.7436436666921,17.0940135709052,
14.6876174970851));
#200674=CARTESIAN_POINT('Ctrl Pts',(-18.759122807348,17.0941276762233,14.6885479230633));
#200675=CARTESIAN_POINT('Ctrl Pts',(-18.7686397536842,17.0942620205944,
14.6891220229911));
#200676=CARTESIAN_POINT('Ctrl Pts',(-18.8009696848581,17.094936489212,14.6910794357538));
#200677=CARTESIAN_POINT('Ctrl Pts',(-18.8237740953053,17.0957812717743,
14.6924722350018));
#200678=CARTESIAN_POINT('Ctrl Pts',(-19.0240757495337,17.1064462853124,
14.7048165381823));
#200679=CARTESIAN_POINT('Ctrl Pts',(-19.1996626756419,17.1382182413091,
14.7164925876397));
#200680=CARTESIAN_POINT('Ctrl Pts',(-19.4506665592065,17.21716552418,14.7338755326956));
#200681=CARTESIAN_POINT('Ctrl Pts',(-19.5305375956243,17.2477077121202,
14.7395018360911));
#200682=CARTESIAN_POINT('Ctrl Pts',(-19.642427065061,17.2984494911567,14.7473430319348));
#200683=CARTESIAN_POINT('Ctrl Pts',(-19.6760922456736,17.3148059751004,
14.7496961544111));
#200684=CARTESIAN_POINT('Ctrl Pts',(-19.7160080817448,17.3355250981281,
14.7524634582063));
#200685=CARTESIAN_POINT('Ctrl Pts',(-19.722689272465,17.3390385937155,14.7529258720062));
#200686=CARTESIAN_POINT('Ctrl Pts',(-19.733038341259,17.3445518111275,14.7536407560317));
#200687=CARTESIAN_POINT('Ctrl Pts',(-19.7367192565435,17.3465267386462,
14.7538947486429));
#200688=CARTESIAN_POINT('Ctrl Pts',(-19.7435300028927,17.3502069227107,
14.7543641637826));
#200689=CARTESIAN_POINT('Ctrl Pts',(-19.7466613454354,17.3519091730141,
14.7545797666228));
#200690=CARTESIAN_POINT('Ctrl Pts',(-19.7537247522056,17.3557721006553,
14.7550656242847));
#200691=CARTESIAN_POINT('Ctrl Pts',(-19.7576542446953,17.3579373683178,
14.7553355818773));
#200692=CARTESIAN_POINT('Ctrl Pts',(-19.7692143336081,17.364355314756,14.7561288690103));
#200693=CARTESIAN_POINT('Ctrl Pts',(-19.7768256325251,17.368642809837,14.7566500249774));
#200694=CARTESIAN_POINT('Ctrl Pts',(-19.8310962808917,17.3996579064673,
14.7603593128213));
#200695=CARTESIAN_POINT('Ctrl Pts',(-19.8767530756473,17.4281099643231,
14.763444415524));
#200696=CARTESIAN_POINT('Ctrl Pts',(-20.060828040386,17.5528005500119,14.7759434955053));
#200697=CARTESIAN_POINT('Ctrl Pts',(-20.1885934942876,17.6636591893677,
14.784813366385));
#200698=CARTESIAN_POINT('Ctrl Pts',(-20.3564535217846,17.8486734027204,
14.7986577457812));
#200699=CARTESIAN_POINT('Ctrl Pts',(-20.4075288885854,17.9119279615835,
14.8032488516325));
#200700=CARTESIAN_POINT('Ctrl Pts',(-20.4662740171239,17.9939128733161,
14.8091327019448));
#200701=CARTESIAN_POINT('Ctrl Pts',(-20.4774848031288,18.0100274577334,
14.8102859877114));
#200702=CARTESIAN_POINT('Ctrl Pts',(-20.4933402564473,18.0335083378921,
14.8119629356255));
#200703=CARTESIAN_POINT('Ctrl Pts',(-20.4981663235767,18.040751337707,14.8124797351089));
#200704=CARTESIAN_POINT('Ctrl Pts',(-20.5065035623441,18.0534327133854,
14.8133838357586));
#200705=CARTESIAN_POINT('Ctrl Pts',(-20.5100347317634,18.0588578509156,
14.8137703807055));
#200706=CARTESIAN_POINT('Ctrl Pts',(-20.5168105272164,18.0693730644883,
14.8145191879849));
#200707=CARTESIAN_POINT('Ctrl Pts',(-20.5200583773066,18.0744609960414,
14.8148813251217));
#200708=CARTESIAN_POINT('Ctrl Pts',(-20.5277198435358,18.0865770382444,
14.8157432930968));
#200709=CARTESIAN_POINT('Ctrl Pts',(-20.5321139550627,18.093617310158,14.8162438398055));
#200710=CARTESIAN_POINT('Ctrl Pts',(-20.5475456171176,18.1186687666544,
14.8180239379527));
#200711=CARTESIAN_POINT('Ctrl Pts',(-20.5583545759495,18.1368186562927,
14.8193118195202));
#200712=CARTESIAN_POINT('Ctrl Pts',(-20.6657649922623,18.3234757962044,
14.8325424656076));
#200713=CARTESIAN_POINT('Ctrl Pts',(-20.7389930069559,18.5043270849297,
14.8453729429948));
#200714=CARTESIAN_POINT('Ctrl Pts',(-20.8048202111708,18.7649445267654,
14.8631017993519));
#200715=CARTESIAN_POINT('Ctrl Pts',(-20.8192617635743,18.8382443946001,
14.8679935684156));
#200716=CARTESIAN_POINT('Ctrl Pts',(-20.8346727882789,18.946323213088,14.8749434265609));
#200717=CARTESIAN_POINT('Ctrl Pts',(-20.8387085621401,18.980604359859,14.8771093787115));
#200718=CARTESIAN_POINT('Ctrl Pts',(-20.8425871754926,19.0223111894511,
14.8796858371126));
#200719=CARTESIAN_POINT('Ctrl Pts',(-20.843231455777,19.0296549876144,14.8801373014638));
#200720=CARTESIAN_POINT('Ctrl Pts',(-20.8441775334707,19.0411267947871,
14.8808389426141));
#200721=CARTESIAN_POINT('Ctrl Pts',(-20.844505601445,19.0452524945572,14.881090554214));
#200722=CARTESIAN_POINT('Ctrl Pts',(-20.8450939760331,19.052936861581,14.8815578121315));
#200723=CARTESIAN_POINT('Ctrl Pts',(-20.8453573820908,19.0564951886913,
14.8817736246496));
#200724=CARTESIAN_POINT('Ctrl Pts',(-20.8459354331728,19.0645816665432,
14.8822628208867));
#200725=CARTESIAN_POINT('Ctrl Pts',(-20.8462445117251,19.0691101630434,
14.8825358896815));
#200726=CARTESIAN_POINT('Ctrl Pts',(-20.8470081049079,19.0808538765501,
14.8832418226054));
#200727=CARTESIAN_POINT('Ctrl Pts',(-20.8474402335298,19.0880705586828,
14.8836734627217));
#200728=CARTESIAN_POINT('Ctrl Pts',(-20.8499256632875,19.1334751345946,
14.8863763467585));
#200729=CARTESIAN_POINT('Ctrl Pts',(-20.8509809805369,19.1717131791939,
14.8885955874458));
#200730=CARTESIAN_POINT('Ctrl Pts',(-20.8510792905107,19.3720991524381,
14.9000237387125));
#200731=CARTESIAN_POINT('Ctrl Pts',(-20.8325322797143,19.5337232380872,
14.9085853799334));
#200732=CARTESIAN_POINT('Ctrl Pts',(-20.7763041605286,19.7749056753729,
14.9221736593812));
#200733=CARTESIAN_POINT('Ctrl Pts',(-20.7518791101994,19.8568712118476,
14.9269356407186));
#200734=CARTESIAN_POINT('Ctrl Pts',(-20.7225805830531,19.9371103667517,
14.9318515409431));
#200735=CARTESIAN_POINT('Origin',(-18.734,19.211,0.));
#200736=CARTESIAN_POINT('',(-20.7225806064913,19.9371103025619,15.9575278864865));
#200737=CARTESIAN_POINT('',(-20.7225806013824,19.9371103165536,15.7328936098053));
#200738=CARTESIAN_POINT('',(-20.7225806064498,19.9371103026755,0.));
#200739=CARTESIAN_POINT('',(-20.8509995343428,19.2095958660383,15.9109437209775));
#200740=CARTESIAN_POINT('Ctrl Pts',(-20.7225806064913,19.9371103025619,
15.9575278864865));
#200741=CARTESIAN_POINT('Ctrl Pts',(-20.7279986629112,19.9222720033623,
15.9565688725157));
#200742=CARTESIAN_POINT('Ctrl Pts',(-20.7332504094381,19.907373693078,15.9556043363318));
#200743=CARTESIAN_POINT('Ctrl Pts',(-20.7683512912222,19.804127365591,15.9489076438136));
#200744=CARTESIAN_POINT('Ctrl Pts',(-20.7924972887047,19.7139614040123,
15.9429901615334));
#200745=CARTESIAN_POINT('Ctrl Pts',(-20.8375635127319,19.4865404276235,
15.9279396372871));
#200746=CARTESIAN_POINT('Ctrl Pts',(-20.8510859005584,19.3482705920783,
15.918664069312));
#200747=CARTESIAN_POINT('Ctrl Pts',(-20.8509995894496,19.2096815653012,
15.9096291633589));
#200748=CARTESIAN_POINT('Ctrl Pts',(-20.7225806064499,19.9371103026755,
15.1555945416419));
#200749=CARTESIAN_POINT('Ctrl Pts',(-20.6976334977237,20.0054323419264,
15.1599719904749));
#200750=CARTESIAN_POINT('Ctrl Pts',(-20.6691305497313,20.0725514062275,
15.1643494393079));
#200751=CARTESIAN_POINT('Ctrl Pts',(-20.6372132630012,20.1380751186049,
15.1687268881409));
#200752=CARTESIAN_POINT('Ctrl Pts',(-20.605318799863,20.2035519759197,15.1731012067233));
#200753=CARTESIAN_POINT('Ctrl Pts',(-20.570015052495,20.2674353123198,15.1774755253057));
#200754=CARTESIAN_POINT('Ctrl Pts',(-20.5314915547277,20.3293528560712,
15.1818498438881));
#200755=CARTESIAN_POINT('Ctrl Pts',(-20.4929828962544,20.3912465491161,
15.1862224774781));
#200756=CARTESIAN_POINT('Ctrl Pts',(-20.4512572037269,20.4511755433295,
15.1905951110682));
#200757=CARTESIAN_POINT('Ctrl Pts',(-20.4065490386169,20.5087937869406,
15.1949677446582));
#200758=CARTESIAN_POINT('Ctrl Pts',(-20.3618433470109,20.5664088427907,
15.1993401363299));
#200759=CARTESIAN_POINT('Ctrl Pts',(-20.3141558073646,20.6217130217184,
15.2037125280016));
#200760=CARTESIAN_POINT('Ctrl Pts',(-20.2637622094331,20.6743921492854,
15.2080849196733));
#200761=CARTESIAN_POINT('Ctrl Pts',(-20.2133189270891,20.7271232146306,
15.2124616222043));
#200762=CARTESIAN_POINT('Ctrl Pts',(-20.1601645909933,20.7772237090099,
15.2168383247353));
#200763=CARTESIAN_POINT('Ctrl Pts',(-20.1046123748413,20.824415853998,15.2212150272663));
#200764=CARTESIAN_POINT('Ctrl Pts',(-20.0490338494289,20.8716303489571,
15.2255938025824));
#200765=CARTESIAN_POINT('Ctrl Pts',(-19.9910555653989,20.9159334570895,
15.2299725778985));
#200766=CARTESIAN_POINT('Ctrl Pts',(-19.9310221853144,20.9570890263286,
15.2343513532146));
#200767=CARTESIAN_POINT('Ctrl Pts',(-19.8708776387445,20.9983208051694,
15.2387382369042));
#200768=CARTESIAN_POINT('Ctrl Pts',(-19.8086708046917,21.0363931464871,
15.2431251205937));
#200769=CARTESIAN_POINT('Ctrl Pts',(-19.7447732573725,21.0711146260864,
15.2475120042832));
#200770=CARTESIAN_POINT('Ctrl Pts',(-19.6856843426586,21.1032231284133,
15.2515687514834));
#200771=CARTESIAN_POINT('Ctrl Pts',(-19.6251501510711,21.1324665213767,
15.2556254986837));
#200772=CARTESIAN_POINT('Ctrl Pts',(-19.5634785608969,21.1587305555473,
15.2596822458839));
#200773=CARTESIAN_POINT('Ctrl Pts',(-19.496768014386,21.1871405262996,15.2640704548148));
#200774=CARTESIAN_POINT('Ctrl Pts',(-19.4284659821155,21.2121746938962,
15.2684586637457));
#200775=CARTESIAN_POINT('Ctrl Pts',(-19.358947687674,21.2336540454736,15.2728468726766));
#200776=CARTESIAN_POINT('Ctrl Pts',(-19.2895325699079,21.255101518132,15.2772285687779));
#200777=CARTESIAN_POINT('Ctrl Pts',(-19.2189052304801,21.273004507002,15.2816102648792));
#200778=CARTESIAN_POINT('Ctrl Pts',(-19.1474611885822,21.2872318862632,
15.2859919609804));
#200779=CARTESIAN_POINT('Ctrl Pts',(-19.0761010991192,21.3014425472216,
15.2903685082401));
#200780=CARTESIAN_POINT('Ctrl Pts',(-19.0039266843577,21.3119860848152,
15.2947450554997));
#200781=CARTESIAN_POINT('Ctrl Pts',(-18.9313473123127,21.31878154426,15.2991216027594));
#200782=CARTESIAN_POINT('Ctrl Pts',(-18.8588139690506,21.3255726941231,
15.3034953744764));
#200783=CARTESIAN_POINT('Ctrl Pts',(-18.7858766571609,21.3286204372107,
15.3078691461933));
#200784=CARTESIAN_POINT('Ctrl Pts',(-18.7129521899224,21.3278953657871,
15.3122429179103));
#200785=CARTESIAN_POINT('Ctrl Pts',(-18.6400499138441,21.3271705150052,
15.3166153586739));
#200786=CARTESIAN_POINT('Ctrl Pts',(-18.567160956721,21.3226751337981,15.3209877994374));
#200787=CARTESIAN_POINT('Ctrl Pts',(-18.4947027860641,21.3144319203156,
15.325360240201));
#200788=CARTESIAN_POINT('Ctrl Pts',(-18.4222427626439,21.3061884960532,
15.3297327927683));
#200789=CARTESIAN_POINT('Ctrl Pts',(-18.3502140266197,21.294197105762,15.3341053453357));
#200790=CARTESIAN_POINT('Ctrl Pts',(-18.2790278943158,21.2785321963755,
15.338477897903));
#200791=CARTESIAN_POINT('Ctrl Pts',(-18.2077678823586,21.2628510293552,
15.3428549884704));
#200792=CARTESIAN_POINT('Ctrl Pts',(-18.1373526922057,21.2434888351845,
15.3472320790377));
#200793=CARTESIAN_POINT('Ctrl Pts',(-18.0681816040659,21.2205708157803,
15.351609169605));
#200794=CARTESIAN_POINT('Ctrl Pts',(-17.9989727390276,21.197640279995,15.355988650664));
#200795=CARTESIAN_POINT('Ctrl Pts',(-17.9310097785368,21.1711502278389,
15.3603681317229));
#200796=CARTESIAN_POINT('Ctrl Pts',(-17.8646724802105,21.1412742456285,
15.3647476127819));
#200797=CARTESIAN_POINT('Ctrl Pts',(-17.7982175994683,21.1113453084402,
15.3691348564416));
#200798=CARTESIAN_POINT('Ctrl Pts',(-17.7333945644596,21.0780186771212,
15.3735221001013));
#200799=CARTESIAN_POINT('Ctrl Pts',(-17.670558444311,21.0415138780227,15.3779093437611));
#200800=CARTESIAN_POINT('Ctrl Pts',(-17.6278359374847,21.0166941322301,
15.3808922466959));
#200801=CARTESIAN_POINT('Ctrl Pts',(-17.5860313573347,20.9904061565717,
15.3838751496306));
#200802=CARTESIAN_POINT('Ctrl Pts',(-17.5452478505358,20.9627298099719,
15.3868580525654));
#200803=CARTESIAN_POINT('Ctrl Pts',(-17.4852504075478,20.9220145758597,
15.3912462614963));
#200804=CARTESIAN_POINT('Ctrl Pts',(-17.4272300397246,20.8781338958608,
15.3956344704272));
#200805=CARTESIAN_POINT('Ctrl Pts',(-17.3715403699668,20.831306377365,15.4000226793581));
#200806=CARTESIAN_POINT('Ctrl Pts',(-17.3159333529124,20.7845483586708,
15.4044043754594));
#200807=CARTESIAN_POINT('Ctrl Pts',(-17.2626505332034,20.7348524915492,
15.4087860715606));
#200808=CARTESIAN_POINT('Ctrl Pts',(-17.2120162539405,20.6824803691285,
15.4131677676619));
#200809=CARTESIAN_POINT('Ctrl Pts',(-17.1614414739853,20.6301697881196,
15.4175443149215));
#200810=CARTESIAN_POINT('Ctrl Pts',(-17.1135093856058,20.5751895440795,
15.4219208621812));
#200811=CARTESIAN_POINT('Ctrl Pts',(-17.0685096421063,20.5178400314358,
15.4262974094408));
#200812=CARTESIAN_POINT('Ctrl Pts',(-17.0235384367902,20.4605268890196,
15.4306711811578));
#200813=CARTESIAN_POINT('Ctrl Pts',(-16.981496183609,20.4008478378287,15.4350449528747));
#200814=CARTESIAN_POINT('Ctrl Pts',(-16.942633222937,20.3391374340189,15.4394187245917));
#200815=CARTESIAN_POINT('Ctrl Pts',(-16.9037820883944,20.2774458088923,
15.4437911653552));
#200816=CARTESIAN_POINT('Ctrl Pts',(-16.8681085825377,20.2137244662937,
15.4481636061188));
#200817=CARTESIAN_POINT('Ctrl Pts',(-16.835819587061,20.1483367164125,15.4525360468823));
#200818=CARTESIAN_POINT('Ctrl Pts',(-16.8035297659512,20.0829472945593,
15.4569085994497));
#200819=CARTESIAN_POINT('Ctrl Pts',(-16.7746248388306,20.0158918142278,
15.461281152017));
#200820=CARTESIAN_POINT('Ctrl Pts',(-16.7492648453346,19.9475564240677,
15.4656537045843));
#200821=CARTESIAN_POINT('Ctrl Pts',(-16.7238785322808,19.8791501128621,
15.4700307951517));
#200822=CARTESIAN_POINT('Ctrl Pts',(-16.7020446665446,19.8094616929176,
15.474407885719));
#200823=CARTESIAN_POINT('Ctrl Pts',(-16.6838740959316,19.7388946651254,
15.4787849762863));
#200824=CARTESIAN_POINT('Ctrl Pts',(-16.6656936016957,19.6682890980602,
15.4831644573452));
#200825=CARTESIAN_POINT('Ctrl Pts',(-16.6511804819231,19.5968044408508,
15.4875439384042));
#200826=CARTESIAN_POINT('Ctrl Pts',(-16.6403943335876,19.5248539685361,
15.4919234194631));
#200827=CARTESIAN_POINT('Ctrl Pts',(-16.6295890668765,19.4527759644922,
15.4963106631228));
#200828=CARTESIAN_POINT('Ctrl Pts',(-16.6225240103778,19.3802309770744,
15.5006979067825));
#200829=CARTESIAN_POINT('Ctrl Pts',(-16.6192067693547,19.3076363886775,
15.5050851504423));
#200830=CARTESIAN_POINT('Ctrl Pts',(-16.6169513651075,19.2582790637646,
15.5080680533771));
#200831=CARTESIAN_POINT('Ctrl Pts',(-16.6164273661252,19.2088988449423,
15.511050956312));
#200832=CARTESIAN_POINT('Ctrl Pts',(-16.6176234550289,19.1596256883618,
15.5140338592469));
#200833=CARTESIAN_POINT('Ctrl Pts',(-16.6193830456439,19.0871389496106,
15.5184220681777));
#200834=CARTESIAN_POINT('Ctrl Pts',(-16.6248744285954,19.014601222373,15.5228102771086));
#200835=CARTESIAN_POINT('Ctrl Pts',(-16.6341051990331,18.9424281755802,
15.5271984860395));
#200836=CARTESIAN_POINT('Ctrl Pts',(-16.643322269477,18.8703622455554,15.5315801821408));
#200837=CARTESIAN_POINT('Ctrl Pts',(-16.6562676494649,18.7986603960529,
15.5359618782421));
#200838=CARTESIAN_POINT('Ctrl Pts',(-16.6728969413427,18.7277369436906,
15.5403435743433));
#200839=CARTESIAN_POINT('Ctrl Pts',(-16.6895066924791,18.6568968320292,
15.544720121603));
#200840=CARTESIAN_POINT('Ctrl Pts',(-16.7097916465688,18.5868337678032,
15.5490966688626));
#200841=CARTESIAN_POINT('Ctrl Pts',(-16.7336560032764,18.5179539014094,
15.5534732161222));
#200842=CARTESIAN_POINT('Ctrl Pts',(-16.7575052255558,18.4491177176257,
15.5578469878392));
#200843=CARTESIAN_POINT('Ctrl Pts',(-16.7849291889402,18.3814636975243,
15.5622207595562));
#200844=CARTESIAN_POINT('Ctrl Pts',(-16.8157820891437,18.315383426644,15.5665945312732));
#200845=CARTESIAN_POINT('Ctrl Pts',(-16.846625600706,18.249323264212,15.5709669720367));
#200846=CARTESIAN_POINT('Ctrl Pts',(-16.8808957735917,18.1848363370635,
15.5753394128003));
#200847=CARTESIAN_POINT('Ctrl Pts',(-16.9183991025639,18.1222932528779,
15.5797118535638));
#200848=CARTESIAN_POINT('Ctrl Pts',(-16.9559033905003,18.0597485694587,
15.5840844061312));
#200849=CARTESIAN_POINT('Ctrl Pts',(-16.9966407488743,17.9991482403585,
15.5884569586985));
#200850=CARTESIAN_POINT('Ctrl Pts',(-17.0403731142,17.9408358485238,15.5928295112658));
#200851=CARTESIAN_POINT('Ctrl Pts',(-17.084150866624,17.8824629378893,15.5972066018332));
#200852=CARTESIAN_POINT('Ctrl Pts',(-17.1309295419548,17.8263830921187,
15.6015836924005));
#200853=CARTESIAN_POINT('Ctrl Pts',(-17.1804298596133,17.7729079240539,
15.6059607829678));
#200854=CARTESIAN_POINT('Ctrl Pts',(-17.2299572112324,17.7194035512151,
15.6103402640267));
#200855=CARTESIAN_POINT('Ctrl Pts',(-17.2822088187836,17.6685070251037,
15.6147197450857));
#200856=CARTESIAN_POINT('Ctrl Pts',(-17.3368694420728,17.6204921552831,
15.6190992261446));
#200857=CARTESIAN_POINT('Ctrl Pts',(-17.3916269509498,17.5723921794281,
15.6234864698043));
#200858=CARTESIAN_POINT('Ctrl Pts',(-17.4488016237918,17.5271843592174,
15.6278737134641));
#200859=CARTESIAN_POINT('Ctrl Pts',(-17.5080466246416,17.4851010106477,
15.6322609571238));
#200860=CARTESIAN_POINT('Ctrl Pts',(-17.548327516385,17.456488388762,15.6352438600586));
#200861=CARTESIAN_POINT('Ctrl Pts',(-17.5895648351145,17.4293192126642,
15.6382267629935));
#200862=CARTESIAN_POINT('Ctrl Pts',(-17.6316431823901,17.4036543090297,
15.6412096659283));
#200863=CARTESIAN_POINT('Ctrl Pts',(-17.6935454914314,17.3658981494093,
15.6455978748592));
#200864=CARTESIAN_POINT('Ctrl Pts',(-17.7575106221335,17.3312522374744,
15.6499860837901));
#200865=CARTESIAN_POINT('Ctrl Pts',(-17.8231931738166,17.2999479532525,
15.654374292721));
#200866=CARTESIAN_POINT('Ctrl Pts',(-17.8887782417026,17.2686901297788,
15.6587559888223));
#200867=CARTESIAN_POINT('Ctrl Pts',(-17.9560752387296,17.2407642944953,
15.6631376849235));
#200868=CARTESIAN_POINT('Ctrl Pts',(-18.0247117585807,17.2163573777279,
15.6675193810248));
#200869=CARTESIAN_POINT('Ctrl Pts',(-18.0932676250587,17.1919791410302,
15.6718959282845));
#200870=CARTESIAN_POINT('Ctrl Pts',(-18.1631594352667,17.1711117694416,
15.6762724755441));
#200871=CARTESIAN_POINT('Ctrl Pts',(-18.2339938260914,17.1538945515474,
15.6806490228038));
#200872=CARTESIAN_POINT('Ctrl Pts',(-18.3047832947748,17.1366882525626,
15.6850227945208));
#200873=CARTESIAN_POINT('Ctrl Pts',(-18.3765136904429,17.1231276279117,
15.6893965662377));
#200874=CARTESIAN_POINT('Ctrl Pts',(-18.4487768305323,17.1133020370895,
15.6937703379547));
#200875=CARTESIAN_POINT('Ctrl Pts',(-18.5210179807056,17.1034794362276,
15.6981427787183));
#200876=CARTESIAN_POINT('Ctrl Pts',(-18.593791075758,17.0973896776779,15.7025152194818));
#200877=CARTESIAN_POINT('Ctrl Pts',(-18.6666797525663,17.0950706570669,
15.7068876602454));
#200878=CARTESIAN_POINT('Ctrl Pts',(-18.7395702931461,17.0927515771582,
15.7112602128128));
#200879=CARTESIAN_POINT('Ctrl Pts',(-18.8125759391522,17.0942034399582,
15.7156327653801));
#200880=CARTESIAN_POINT('Ctrl Pts',(-18.8852789324501,17.0994120466822,
15.7200053179475));
#200881=CARTESIAN_POINT('Ctrl Pts',(-18.9580573796568,17.1046260590948,
15.7243824085148));
#200882=CARTESIAN_POINT('Ctrl Pts',(-19.0305320648508,17.113604565285,15.7287594990821));
#200883=CARTESIAN_POINT('Ctrl Pts',(-19.1022898016653,17.1262814046041,
15.7331365896495));
#200884=CARTESIAN_POINT('Ctrl Pts',(-19.1740867280431,17.1389651672157,
15.7375160707084));
#200885=CARTESIAN_POINT('Ctrl Pts',(-19.2451654560904,17.155351175915,15.7418955517674));
#200886=CARTESIAN_POINT('Ctrl Pts',(-19.3151251217573,17.1753225715103,
15.7462750328263));
#200887=CARTESIAN_POINT('Ctrl Pts',(-19.3852087904621,17.1953293662702,
15.750662276486));
#200888=CARTESIAN_POINT('Ctrl Pts',(-19.4541689789727,17.2189340823964,
15.7550495201458));
#200889=CARTESIAN_POINT('Ctrl Pts',(-19.5216226105752,17.2459708339796,
15.7594367638055));
#200890=CARTESIAN_POINT('Ctrl Pts',(-19.5674845802476,17.2643532198007,
15.7624196667403));
#200891=CARTESIAN_POINT('Ctrl Pts',(-19.61265053623,17.284321119187,15.765402569675));
#200892=CARTESIAN_POINT('Ctrl Pts',(-19.6570068699278,17.3058104246385,
15.7683854726098));
#200893=CARTESIAN_POINT('Ctrl Pts',(-19.7222603709406,17.3374237771891,
15.7727736815407));
#200894=CARTESIAN_POINT('Ctrl Pts',(-19.7860152120978,17.3724551543895,
15.7771618904716));
#200895=CARTESIAN_POINT('Ctrl Pts',(-19.8478898805759,17.4107393705492,
15.7815500994025));
#200896=CARTESIAN_POINT('Ctrl Pts',(-19.9096727167869,17.4489667665845,
15.7859317955037));
#200897=CARTESIAN_POINT('Ctrl Pts',(-19.9695805130033,17.4904371661198,
15.790313491605));
#200898=CARTESIAN_POINT('Ctrl Pts',(-20.0272545139271,17.5349386162174,
15.7946951877063));
#200899=CARTESIAN_POINT('Ctrl Pts',(-20.0848607433099,17.5793877735696,
15.7990717349659));
#200900=CARTESIAN_POINT('Ctrl Pts',(-20.1402380117453,17.6268606128758,
15.8034482822256));
#200901=CARTESIAN_POINT('Ctrl Pts',(-20.1930562795834,17.6771017722782,
15.8078248294852));
#200902=CARTESIAN_POINT('Ctrl Pts',(-20.2458410508437,17.7273110694674,
15.8121986012022));
#200903=CARTESIAN_POINT('Ctrl Pts',(-20.2960696928603,17.780284871717,15.8165723729192));
#200904=CARTESIAN_POINT('Ctrl Pts',(-20.3434461269599,17.8357283306874,
15.8209461446361));
#200905=CARTESIAN_POINT('Ctrl Pts',(-20.3908081442515,17.8911549180271,
15.8253185853997));
#200906=CARTESIAN_POINT('Ctrl Pts',(-20.4353193635675,17.9490493035726,
15.8296910261632));
#200907=CARTESIAN_POINT('Ctrl Pts',(-20.4767225512217,18.009081904012,15.8340634669268));
#200908=CARTESIAN_POINT('Ctrl Pts',(-20.5181267975599,18.0691160394917,
15.8384360194941));
#200909=CARTESIAN_POINT('Ctrl Pts',(-20.5564225822289,18.1312881001857,
15.8428085720615));
#200910=CARTESIAN_POINT('Ctrl Pts',(-20.5913957196047,18.1952391320817,
15.8471811246288));
#200911=CARTESIAN_POINT('Ctrl Pts',(-20.6264051534217,18.2592565347709,
15.8515582151961));
#200912=CARTESIAN_POINT('Ctrl Pts',(-20.6580848230995,18.3250561707613,
15.8559353057635));
#200913=CARTESIAN_POINT('Ctrl Pts',(-20.68626670933,18.3922548042024,15.8603123963308));
#200914=CARTESIAN_POINT('Ctrl Pts',(-20.7144639867346,18.4594901373112,
15.8646918773897));
#200915=CARTESIAN_POINT('Ctrl Pts',(-20.7391595139379,18.52812553487,15.8690713584487));
#200916=CARTESIAN_POINT('Ctrl Pts',(-20.7602345709197,18.597760679987,15.8734508395076));
#200917=CARTESIAN_POINT('Ctrl Pts',(-20.7813469832985,18.6675192529313,
15.8778380831673));
#200918=CARTESIAN_POINT('Ctrl Pts',(-20.7988259946711,18.7382806434225,
15.8822253268271));
#200919=CARTESIAN_POINT('Ctrl Pts',(-20.8126037366755,18.809632953671,15.8866125704868));
#200920=CARTESIAN_POINT('Ctrl Pts',(-20.8219712736183,18.8581456491475,
15.8895954734216));
#200921=CARTESIAN_POINT('Ctrl Pts',(-20.8296289055563,18.9069313156785,
15.8925783763564));
#200922=CARTESIAN_POINT('Ctrl Pts',(-20.8355690425742,18.9558597262409,
15.8955612792912));
#200923=CARTESIAN_POINT('Ctrl Pts',(-20.8457798800574,19.0399655384573,
15.9006887598533));
#200924=CARTESIAN_POINT('Ctrl Pts',(-20.850943223371,19.1246963446804,15.9058162404154));
#200925=CARTESIAN_POINT('Ctrl Pts',(-20.8509995343428,19.2095958660383,
15.9109437209775));
#200926=CARTESIAN_POINT('',(-20.8509995791044,19.2096650574301,15.6876314267646));
#200927=CARTESIAN_POINT('Ctrl Pts',(-20.7225805830531,19.9371103667517,
14.9318515409431));
#200928=CARTESIAN_POINT('Ctrl Pts',(-20.714010105929,19.9605821214281,14.9332895521512));
#200929=CARTESIAN_POINT('Ctrl Pts',(-20.7050225936995,19.983906167217,14.9347403770111));
#200930=CARTESIAN_POINT('Ctrl Pts',(-20.6902873330294,20.0202157299443,
14.9370363167659));
#200931=CARTESIAN_POINT('Ctrl Pts',(-20.6848211921425,20.0333058364495,
14.9378717579225));
#200932=CARTESIAN_POINT('Ctrl Pts',(-20.6758998546064,20.0540806160084,
14.9392104414492));
#200933=CARTESIAN_POINT('Ctrl Pts',(-20.6725295631085,20.0618014458346,
14.9397107969794));
#200934=CARTESIAN_POINT('Ctrl Pts',(-20.6664968926029,20.0753994372095,
14.9405971440495));
#200935=CARTESIAN_POINT('Ctrl Pts',(-20.6638535463858,20.0812849619796,
14.9409824795058));
#200936=CARTESIAN_POINT('Ctrl Pts',(-20.6583232643003,20.0934492798618,
14.9417824755278));
#200937=CARTESIAN_POINT('Ctrl Pts',(-20.6554324089197,20.0997261970076,
14.9421972676894));
#200938=CARTESIAN_POINT('Ctrl Pts',(-20.6479172869637,20.115835720989,14.9432669949786));
#200939=CARTESIAN_POINT('Ctrl Pts',(-20.6432480022968,20.1256469931882,
14.9439234830348));
#200940=CARTESIAN_POINT('Ctrl Pts',(-20.623305148899,20.1667334708388,14.9466939815646));
#200941=CARTESIAN_POINT('Ctrl Pts',(-20.6073377252505,20.1976640533919,
14.9488320641504));
#200942=CARTESIAN_POINT('Ctrl Pts',(-20.563605053731,20.2774870174198,14.9544919100229));
#200943=CARTESIAN_POINT('Ctrl Pts',(-20.5346432922634,20.3256892288278,
14.9580538990754));
#200944=CARTESIAN_POINT('Ctrl Pts',(-20.4347644591281,20.4778530934194,
14.9697637599371));
#200945=CARTESIAN_POINT('Ctrl Pts',(-20.3564950966972,20.5766579015057,
14.9781232382993));
#200946=CARTESIAN_POINT('Ctrl Pts',(-20.2011016309508,20.7404781432947,
14.9930007275872));
#200947=CARTESIAN_POINT('Ctrl Pts',(-20.1272124158796,20.8080768618124,
14.9995202713344));
#200948=CARTESIAN_POINT('Ctrl Pts',(-20.0412146256351,20.8762245784271,
15.0062996210402));
#200949=CARTESIAN_POINT('Ctrl Pts',(-20.0335754802509,20.8821931526325,
15.0068952528871));
#200950=CARTESIAN_POINT('Ctrl Pts',(-20.0222359707755,20.8909281001533,
15.0077694112859));
#200951=CARTESIAN_POINT('Ctrl Pts',(-20.0185672440217,20.8937350755852,
15.0080507032578));
#200952=CARTESIAN_POINT('Ctrl Pts',(-20.0120424371034,20.898693489401,15.0085482293783));
#200953=CARTESIAN_POINT('Ctrl Pts',(-20.0091900673703,20.9008497205265,
15.0087647983666));
#200954=CARTESIAN_POINT('Ctrl Pts',(-20.0030671636054,20.9054539600138,
15.0092276907257));
#200955=CARTESIAN_POINT('Ctrl Pts',(-19.9997950120221,20.9078997249504,
15.0094738578791));
#200956=CARTESIAN_POINT('Ctrl Pts',(-19.9907938675744,20.9145870938001,
15.0101477763432));
#200957=CARTESIAN_POINT('Ctrl Pts',(-19.98505043846,20.9188093030122,15.0105741955297));
#200958=CARTESIAN_POINT('Ctrl Pts',(-19.9542778836496,20.9411928116132,
15.0128404277134));
#200959=CARTESIAN_POINT('Ctrl Pts',(-19.9288730008383,20.9588340932724,
15.0146465059246));
#200960=CARTESIAN_POINT('Ctrl Pts',(-19.8508165748393,21.0105391382306,
15.0200319810482));
#200961=CARTESIAN_POINT('Ctrl Pts',(-19.7970274229189,21.0428281084345,
15.0235246284933));
#200962=CARTESIAN_POINT('Ctrl Pts',(-19.6236648553288,21.1366833539519,
15.0343590003749));
#200963=CARTESIAN_POINT('Ctrl Pts',(-19.4996236594439,21.1892772928256,
15.0415277489855));
#200964=CARTESIAN_POINT('Ctrl Pts',(-19.3325234617007,21.2420399883082,
15.0512527937098));
#200965=CARTESIAN_POINT('Ctrl Pts',(-19.2932699553191,21.253197502654,15.0535400264754));
#200966=CARTESIAN_POINT('Ctrl Pts',(-19.2066104697927,21.275143885851,15.0586207672228));
#200967=CARTESIAN_POINT('Ctrl Pts',(-19.1591071467,21.28544788283,15.0614260732125));
#200968=CARTESIAN_POINT('Ctrl Pts',(-19.0988926621608,21.2963539699619,
15.0650250902967));
#200969=CARTESIAN_POINT('Ctrl Pts',(-19.0864718539404,21.2984892614768,
15.065769734783));
#200970=CARTESIAN_POINT('Ctrl Pts',(-19.0667599268285,21.3016970436467,
15.0669553411896));
#200971=CARTESIAN_POINT('Ctrl Pts',(-19.0594808768274,21.3028426073513,
15.0673939803643));
#200972=CARTESIAN_POINT('Ctrl Pts',(-19.0459068920162,21.3049062917516,
15.0682135567924));
#200973=CARTESIAN_POINT('Ctrl Pts',(-19.0396134959049,21.3058340883414,
15.0685941824011));
#200974=CARTESIAN_POINT('Ctrl Pts',(-19.0256263735261,21.3078317519062,
15.0694415868103));
#200975=CARTESIAN_POINT('Ctrl Pts',(-19.0179307757519,21.3088876637252,
15.0699088019049));
#200976=CARTESIAN_POINT('Ctrl Pts',(-18.9955533400665,21.3118326859083,
15.0712703125729));
#200977=CARTESIAN_POINT('Ctrl Pts',(-18.9808575074943,21.3136101582108,
15.0721681164671));
#200978=CARTESIAN_POINT('Ctrl Pts',(-18.8639363523084,21.3265092061133,
15.0793414941781));
#200979=CARTESIAN_POINT('Ctrl Pts',(-18.7610577403731,21.3303218489948,
15.0858478890049));
#200980=CARTESIAN_POINT('Ctrl Pts',(-18.5026289384204,21.3210776411383,
15.1026341270099));
#200981=CARTESIAN_POINT('Ctrl Pts',(-18.348038087996,21.2983403900046,15.1131044691046));
#200982=CARTESIAN_POINT('Ctrl Pts',(-18.1465315252016,21.2455341593658,
15.12656034383));
#200983=CARTESIAN_POINT('Ctrl Pts',(-18.0962253255101,21.2303298180707,
15.1298980694134));
#200984=CARTESIAN_POINT('Ctrl Pts',(-18.0383148344007,21.2104465849901,
15.1336749021378));
#200985=CARTESIAN_POINT('Ctrl Pts',(-18.0301141804618,21.2075743799977,
15.1342081726498));
#200986=CARTESIAN_POINT('Ctrl Pts',(-18.0177156618509,21.2031460251375,
15.1350117965231));
#200987=CARTESIAN_POINT('Ctrl Pts',(-18.0135047821559,21.2016269566306,
15.1352842686453));
#200988=CARTESIAN_POINT('Ctrl Pts',(-18.0059505305127,21.1988746611253,
15.1357722098489));
#200989=CARTESIAN_POINT('Ctrl Pts',(-18.0026054413987,21.19764634462,15.1359879647496));
#200990=CARTESIAN_POINT('Ctrl Pts',(-17.9953385663123,21.1949571064528,
15.1364559928437));
#200991=CARTESIAN_POINT('Ctrl Pts',(-17.9914180185891,21.1934930051433,
15.1367080731634));
#200992=CARTESIAN_POINT('Ctrl Pts',(-17.9804047479368,21.1893429218316,
15.1374150671293));
#200993=CARTESIAN_POINT('Ctrl Pts',(-17.9733219974898,21.1866304059046,
15.1378684228144));
#200994=CARTESIAN_POINT('Ctrl Pts',(-17.9308014683579,21.1700835429774,
15.1405830127833));
#200995=CARTESIAN_POINT('Ctrl Pts',(-17.8957248758046,21.1553331585878,
15.1427927144636));
#200996=CARTESIAN_POINT('Ctrl Pts',(-17.7810017022344,21.1034074863403,
15.1499808166621));
#200997=CARTESIAN_POINT('Ctrl Pts',(-17.7032682728916,21.0622175463789,
15.1547898674582));
#200998=CARTESIAN_POINT('Ctrl Pts',(-17.4797360629945,20.9253125742143,
15.1690495330684));
#200999=CARTESIAN_POINT('Ctrl Pts',(-17.342976215466,20.8163322713576,15.1784224949014));
#201000=CARTESIAN_POINT('Ctrl Pts',(-17.2049682354818,20.6753373026759,
15.18988602955));
#201001=CARTESIAN_POINT('Ctrl Pts',(-17.1890924266148,20.6585781156718,
15.191238337592));
#201002=CARTESIAN_POINT('Ctrl Pts',(-17.1670331401775,20.6345151145433,
15.1931674499305));
#201003=CARTESIAN_POINT('Ctrl Pts',(-17.1606199011764,20.6274234822899,
15.1937344778527));
#201004=CARTESIAN_POINT('Ctrl Pts',(-17.1502810146679,20.6158340869886,
15.1946588285409));
#201005=CARTESIAN_POINT('Ctrl Pts',(-17.1463259194027,20.6113626848578,
15.1950149097325));
#201006=CARTESIAN_POINT('Ctrl Pts',(-17.1380892785461,20.6019710668898,
15.1957616999097));
#201007=CARTESIAN_POINT('Ctrl Pts',(-17.1338114588514,20.5970476799429,
15.1961525583538));
#201008=CARTESIAN_POINT('Ctrl Pts',(-17.1236935950338,20.5852936532444,
15.1970842349144));
#201009=CARTESIAN_POINT('Ctrl Pts',(-17.1178741955492,20.5784454810042,
15.1976258959164));
#201010=CARTESIAN_POINT('Ctrl Pts',(-17.0984378565033,20.5552757479446,
15.1994548008658));
#201011=CARTESIAN_POINT('Ctrl Pts',(-17.0850235146524,20.5387866209648,
15.2007502338299));
#201012=CARTESIAN_POINT('Ctrl Pts',(-17.0134819528044,20.4480901092409,
15.2078449111842));
#201013=CARTESIAN_POINT('Ctrl Pts',(-16.9601195976993,20.3702749881867,
15.2138292057618));
#201014=CARTESIAN_POINT('Ctrl Pts',(-16.8276109236315,20.1463642895075,
15.2307279303986));
#201015=CARTESIAN_POINT('Ctrl Pts',(-16.7601869832664,19.994124729502,15.2419104978843));
#201016=CARTESIAN_POINT('Ctrl Pts',(-16.698840707698,19.7954482201582,15.2552394432181));
#201017=CARTESIAN_POINT('Ctrl Pts',(-16.6876452440825,19.7549538801397,
15.2578905603053));
#201018=CARTESIAN_POINT('Ctrl Pts',(-16.6758936236268,19.7069258622046,
15.2609373606017));
#201019=CARTESIAN_POINT('Ctrl Pts',(-16.6741639831534,19.6996920346282,
15.2613936779627));
#201020=CARTESIAN_POINT('Ctrl Pts',(-16.6714259028112,19.6879677884871,
15.2621289131939));
#201021=CARTESIAN_POINT('Ctrl Pts',(-16.6703939360781,19.68348300659,15.2624091311566));
#201022=CARTESIAN_POINT('Ctrl Pts',(-16.6685865355233,19.6755094113196,
15.2629054721059));
#201023=CARTESIAN_POINT('Ctrl Pts',(-16.6678053051221,19.6720219690793,
15.2631219239834));
#201024=CARTESIAN_POINT('Ctrl Pts',(-16.6661476064176,19.6645330829273,
15.263585359257));
#201025=CARTESIAN_POINT('Ctrl Pts',(-16.6652739215586,19.6605310801099,
15.2638321822816));
#201026=CARTESIAN_POINT('Ctrl Pts',(-16.662901128459,19.649508830755,15.2645097490968));
#201027=CARTESIAN_POINT('Ctrl Pts',(-16.6614260867731,19.6424833808142,
15.2649391366288));
#201028=CARTESIAN_POINT('Ctrl Pts',(-16.6536456822026,19.6044656053513,
15.2672499832116));
#201029=CARTESIAN_POINT('Ctrl Pts',(-16.6479993385541,19.5733406581219,
15.2690961143121));
#201030=CARTESIAN_POINT('Ctrl Pts',(-16.6174875116691,19.3806531926838,
15.2803086994677));
#201031=CARTESIAN_POINT('Ctrl Pts',(-16.6107039351241,19.2167727713442,
15.2889469574216));
#201032=CARTESIAN_POINT('Ctrl Pts',(-16.6315476406607,18.9369726719341,
15.3043057823969));
#201033=CARTESIAN_POINT('Ctrl Pts',(-16.6499146963895,18.8211537964578,
15.3108410712198));
#201034=CARTESIAN_POINT('Ctrl Pts',(-16.6811576339985,18.6935722119373,
15.3185360417941));
#201035=CARTESIAN_POINT('Ctrl Pts',(-16.684697829224,18.6797242773819,15.3193777412692));
#201036=CARTESIAN_POINT('Ctrl Pts',(-16.6905550861813,18.6577429327706,
15.3207245703816));
#201037=CARTESIAN_POINT('Ctrl Pts',(-16.6927811637243,18.6495855741792,
15.3212267570963));
#201038=CARTESIAN_POINT('Ctrl Pts',(-16.6967932162291,18.6352229486684,
15.3221152349032));
#201039=CARTESIAN_POINT('Ctrl Pts',(-16.6985588333928,18.6290120718283,
15.3225008596541));
#201040=CARTESIAN_POINT('Ctrl Pts',(-16.702269315911,18.6161832156927,15.3233003618797));
#201041=CARTESIAN_POINT('Ctrl Pts',(-16.7042181655002,18.6095664773681,
15.3237143655532));
#201042=CARTESIAN_POINT('Ctrl Pts',(-16.7093033171964,18.5926076182379,
15.3247797495212));
#201043=CARTESIAN_POINT('Ctrl Pts',(-16.7124865111845,18.5822798691535,
15.3254326586177));
#201044=CARTESIAN_POINT('Ctrl Pts',(-16.7260999394291,18.5392840385424,
15.328168264609));
#201045=CARTESIAN_POINT('Ctrl Pts',(-16.73724361527,18.5068489436963,15.3302742831441));
#201046=CARTESIAN_POINT('Ctrl Pts',(-16.7683257266418,18.4230614422431,
15.3358290666946));
#201047=CARTESIAN_POINT('Ctrl Pts',(-16.7894882924941,18.3721937533858,
15.3393162224231));
#201048=CARTESIAN_POINT('Ctrl Pts',(-16.8585267494172,18.2229456383316,
15.3498858931871));
#201049=CARTESIAN_POINT('Ctrl Pts',(-16.9120655957312,18.12739356991,15.3571167986195));
#201050=CARTESIAN_POINT('Ctrl Pts',(-16.9983209755564,17.9980560792936,
15.3673861884883));
#201051=CARTESIAN_POINT('Ctrl Pts',(-17.0251482361426,17.9605438923364,
15.3704260515794));
#201052=CARTESIAN_POINT('Ctrl Pts',(-17.0664504489016,17.9066058976365,
15.3748626788361));
#201053=CARTESIAN_POINT('Ctrl Pts',(-17.0799889566774,17.88948080074,15.3762814686363));
#201054=CARTESIAN_POINT('Ctrl Pts',(-17.1264813801059,17.8325056876575,
15.3810289926653));
#201055=CARTESIAN_POINT('Ctrl Pts',(-17.1606324027548,17.7936510519272,
15.3843127762957));
#201056=CARTESIAN_POINT('Ctrl Pts',(-17.2021191584776,17.7498001868932,
15.3880361031336));
#201057=CARTESIAN_POINT('Ctrl Pts',(-17.208101832978,17.7435537160834,15.3885669035559));
#201058=CARTESIAN_POINT('Ctrl Pts',(-17.2172328403705,17.7341363146082,
15.3893675502721));
#201059=CARTESIAN_POINT('Ctrl Pts',(-17.2203531224792,17.7309384834479,
15.3896394923708));
#201060=CARTESIAN_POINT('Ctrl Pts',(-17.2259798705567,17.725208297314,15.3901268694201));
#201061=CARTESIAN_POINT('Ctrl Pts',(-17.2284826140154,17.7226723829591,
15.3903425872283));
#201062=CARTESIAN_POINT('Ctrl Pts',(-17.2339437067379,17.7171667807001,
15.3908109780318));
#201063=CARTESIAN_POINT('Ctrl Pts',(-17.2369044677119,17.714199566428,15.3910634557459));
#201064=CARTESIAN_POINT('Ctrl Pts',(-17.2452688903829,17.7058665595312,
15.3917726891239));
#201065=CARTESIAN_POINT('Ctrl Pts',(-17.2506927824817,17.7005210386077,
15.3922278709585));
#201066=CARTESIAN_POINT('Ctrl Pts',(-17.2837781783381,17.6682637774233,
15.3949768593752));
#201067=CARTESIAN_POINT('Ctrl Pts',(-17.3121443818488,17.6420814527203,
15.3972176029302));
#201068=CARTESIAN_POINT('Ctrl Pts',(-17.4090615902289,17.5574148150299,
15.4045593427285));
#201069=CARTESIAN_POINT('Ctrl Pts',(-17.4806308105671,17.5025287513374,
15.4094826296095));
#201070=CARTESIAN_POINT('Ctrl Pts',(-17.6976413966474,17.3571031522537,
15.4236874288174));
#201071=CARTESIAN_POINT('Ctrl Pts',(-17.8508055445381,17.2794375843642,
15.4329079072757));
#201072=CARTESIAN_POINT('Ctrl Pts',(-18.0335302010128,17.2131077798765,
15.4442003775982));
#201073=CARTESIAN_POINT('Ctrl Pts',(-18.0555481095039,17.2055239389201,
15.4455643641494));
#201074=CARTESIAN_POINT('Ctrl Pts',(-18.0868081545907,17.1953304395445,
15.4475073060515));
#201075=CARTESIAN_POINT('Ctrl Pts',(-18.0959502928806,17.1924179163705,
15.4480762913423));
#201076=CARTESIAN_POINT('Ctrl Pts',(-18.1108177556226,17.1877924971797,
15.4490029642072));
#201077=CARTESIAN_POINT('Ctrl Pts',(-18.116531154563,17.1860414984591,15.4493593976203));
#201078=CARTESIAN_POINT('Ctrl Pts',(-18.1284909091304,17.1824314866439,
15.4501062222404));
#201079=CARTESIAN_POINT('Ctrl Pts',(-18.1347385804405,17.1805770829557,
15.450496759796));
#201080=CARTESIAN_POINT('Ctrl Pts',(-18.1495942448935,17.1762422348056,
15.4514263774424));
#201081=CARTESIAN_POINT('Ctrl Pts',(-18.1582095642348,17.1737875368911,
15.4519662905354));
#201082=CARTESIAN_POINT('Ctrl Pts',(-18.1871568417086,17.1657380981198,
15.4537831933396));
#201083=CARTESIAN_POINT('Ctrl Pts',(-18.207556255928,17.1603926214685,15.4550682264372));
#201084=CARTESIAN_POINT('Ctrl Pts',(-18.3182055908662,17.133157853292,15.4620656072602));
#201085=CARTESIAN_POINT('Ctrl Pts',(-18.4097304674114,17.1169230415623,
15.4679573707977));
#201086=CARTESIAN_POINT('Ctrl Pts',(-18.6540655821775,17.0899861597897,
15.4839117914373));
#201087=CARTESIAN_POINT('Ctrl Pts',(-18.807473373259,17.089753396508,15.4941848570405));
#201088=CARTESIAN_POINT('Ctrl Pts',(-18.9638676732419,17.106512269825,15.5043643049148));
#201089=CARTESIAN_POINT('Ctrl Pts',(-18.9681721682654,17.1069868941303,
15.5046442125475));
#201090=CARTESIAN_POINT('Ctrl Pts',(-19.0235796242697,17.1132683989512,
15.5082435411218));
#201091=CARTESIAN_POINT('Ctrl Pts',(-19.074460688714,17.1209230423382,15.5115092579736));
#201092=CARTESIAN_POINT('Ctrl Pts',(-19.1327595734839,17.1318795430207,
15.5151679587037));
#201093=CARTESIAN_POINT('Ctrl Pts',(-19.1404945549523,17.1333779811331,
15.5156516791356));
#201094=CARTESIAN_POINT('Ctrl Pts',(-19.1528133496738,17.1358358363388,
15.516419132414));
#201095=CARTESIAN_POINT('Ctrl Pts',(-19.1574025703433,17.136767324429,15.5167043894806));
#201096=CARTESIAN_POINT('Ctrl Pts',(-19.1655075977397,17.1384404463791,
15.5172069892166));
#201097=CARTESIAN_POINT('Ctrl Pts',(-19.1690246550353,17.1391758133299,
15.5174246858046));
#201098=CARTESIAN_POINT('Ctrl Pts',(-19.1764559265738,17.1407493446699,
15.5178838029626));
#201099=CARTESIAN_POINT('Ctrl Pts',(-19.1803696336362,17.1415896555699,
15.5181250990765));
#201100=CARTESIAN_POINT('Ctrl Pts',(-19.1908835030481,17.1438782997365,
15.5187720356665));
#201101=CARTESIAN_POINT('Ctrl Pts',(-19.1974792178293,17.1453471548894,
15.5191765166686));
#201102=CARTESIAN_POINT('Ctrl Pts',(-19.2296418826757,17.1526715345459,
15.5211427177802));
#201103=CARTESIAN_POINT('Ctrl Pts',(-19.255106768312,17.1589705591677,15.5226804089078));
#201104=CARTESIAN_POINT('Ctrl Pts',(-19.3276967081876,17.1783650379128,
15.5270260421735));
#201105=CARTESIAN_POINT('Ctrl Pts',(-19.374495716819,17.1926227964102,15.5297818683856));
#201106=CARTESIAN_POINT('Ctrl Pts',(-19.5505236671568,17.2529916510873,
15.5401147113778));
#201107=CARTESIAN_POINT('Ctrl Pts',(-19.6756557403249,17.3100016040193,
15.5474115978392));
#201108=CARTESIAN_POINT('Ctrl Pts',(-19.8818239945251,17.4293174094384,
15.5605317142495));
#201109=CARTESIAN_POINT('Ctrl Pts',(-19.965508211468,17.4861010100236,15.5662145003484));
#201110=CARTESIAN_POINT('Ctrl Pts',(-20.055831543385,17.5573231187063,15.5729553902449));
#201111=CARTESIAN_POINT('Ctrl Pts',(-20.0667621388542,17.566119784323,15.5737818339964));
#201112=CARTESIAN_POINT('Ctrl Pts',(-20.0840796475392,17.5803424155024,
15.5751087993495));
#201113=CARTESIAN_POINT('Ctrl Pts',(-20.0905232966979,17.5856988725117,
15.5756065138542));
#201114=CARTESIAN_POINT('Ctrl Pts',(-20.1018663217547,17.5952425120317,
15.5764897966285));
#201115=CARTESIAN_POINT('Ctrl Pts',(-20.1067787224529,17.5994141003721,
15.5768747235754));
#201116=CARTESIAN_POINT('Ctrl Pts',(-20.1118623973303,17.6037712431229,
15.5772755922498));
#201117=CARTESIAN_POINT('Ctrl Pts',(-20.1120528087966,17.6039345006879,
15.5772906106666));
#201118=CARTESIAN_POINT('Ctrl Pts',(-20.1123584314734,17.6041966338607,
15.5773147221196));
#201119=CARTESIAN_POINT('Ctrl Pts',(-20.1124736596305,17.6042954867946,
15.5773238141534));
#201120=CARTESIAN_POINT('Ctrl Pts',(-20.1127006051659,17.6044902231886,
15.5773417238694));
#201121=CARTESIAN_POINT('Ctrl Pts',(-20.1128123241027,17.6045861067036,
15.577350541594));
#201122=CARTESIAN_POINT('Ctrl Pts',(-20.1130253202141,17.6047689506089,
15.577367355325));
#201123=CARTESIAN_POINT('Ctrl Pts',(-20.1131266017917,17.6048559111805,
15.5773753514527));
#201124=CARTESIAN_POINT('Ctrl Pts',(-20.113319853976,17.6050218696612,15.5773906106093));
#201125=CARTESIAN_POINT('Ctrl Pts',(-20.1134118267743,17.6051008665382,
15.577397873628));
#201126=CARTESIAN_POINT('Ctrl Pts',(-20.1135874428174,17.6052517321257,
15.5774117435363));
#201127=CARTESIAN_POINT('Ctrl Pts',(-20.1136710883106,17.6053236003969,
15.5774183504544));
#201128=CARTESIAN_POINT('Ctrl Pts',(-20.113830917418,17.6054609473987,15.5774309762642));
#201129=CARTESIAN_POINT('Ctrl Pts',(-20.1139070984954,17.6055264220136,
15.5774369948338));
#201130=CARTESIAN_POINT('Ctrl Pts',(-20.1140527497211,17.6056516214914,
15.5774485029204));
#201131=CARTESIAN_POINT('Ctrl Pts',(-20.1141222206594,17.6057113454474,
15.5774539924001));
#201132=CARTESIAN_POINT('Ctrl Pts',(-20.1142551174675,17.6058256114358,
15.5774644946323));
#201133=CARTESIAN_POINT('Ctrl Pts',(-20.1143185439812,17.6058801527177,
15.5774695073536));
#201134=CARTESIAN_POINT('Ctrl Pts',(-20.1144399406737,17.6059845558252,
15.5774791023592));
#201135=CARTESIAN_POINT('Ctrl Pts',(-20.1144979113635,17.6060344170146,
15.5774836846161));
#201136=CARTESIAN_POINT('Ctrl Pts',(-20.1146089183281,17.6061299057158,
15.5774924597509));
#201137=CARTESIAN_POINT('Ctrl Pts',(-20.1146619551019,17.6061755327672,
15.5774966526122));
#201138=CARTESIAN_POINT('Ctrl Pts',(-20.1147635586412,17.6062629501274,
15.5775046855067));
#201139=CARTESIAN_POINT('Ctrl Pts',(-20.1148121257641,17.6063047400058,
15.5775085255217));
#201140=CARTESIAN_POINT('Ctrl Pts',(-20.1149052038986,17.606384837011,15.5775158853136));
#201141=CARTESIAN_POINT('Ctrl Pts',(-20.1149497152654,17.6064231438297,
15.5775194050799));
#201142=CARTESIAN_POINT('Ctrl Pts',(-20.1150350525118,17.6064965918904,
15.5775261535694));
#201143=CARTESIAN_POINT('Ctrl Pts',(-20.1150758784476,17.6065317326691,
15.5775293822648));
#201144=CARTESIAN_POINT('Ctrl Pts',(-20.1151740831899,17.6066162685763,
15.5775371491405));
#201145=CARTESIAN_POINT('Ctrl Pts',(-20.1152314607782,17.6066656653034,
15.5775416873913));
#201146=CARTESIAN_POINT('Ctrl Pts',(-20.1153451301596,17.6067635346051,
15.5775506786807));
#201147=CARTESIAN_POINT('Ctrl Pts',(-20.1154014279276,17.6068120121257,
15.5775551321793));
#201148=CARTESIAN_POINT('Ctrl Pts',(-20.1155129909783,17.6069080883325,
15.5775639581452));
#201149=CARTESIAN_POINT('Ctrl Pts',(-20.1155682502987,17.6069556816954,
15.5775683301287));
#201150=CARTESIAN_POINT('Ctrl Pts',(-20.115677762143,17.6070500111515,15.5775769950612));
#201151=CARTESIAN_POINT('Ctrl Pts',(-20.1157320148557,17.6070967472287,
15.5775812880138));
#201152=CARTESIAN_POINT('Ctrl Pts',(-20.1158395463032,17.6071893898534,
15.5775897974481));
#201153=CARTESIAN_POINT('Ctrl Pts',(-20.1158928250621,17.607235296252,15.5775940139209));
#201154=CARTESIAN_POINT('Ctrl Pts',(-20.1159984397161,17.6073263058229,
15.5776023728261));
#201155=CARTESIAN_POINT('Ctrl Pts',(-20.1160507757332,17.6073714089389,
15.5776065152579));
#201156=CARTESIAN_POINT('Ctrl Pts',(-20.1161545350013,17.6074608374023,
15.5776147284331));
#201157=CARTESIAN_POINT('Ctrl Pts',(-20.1162059583187,17.6075051626533,
15.577618799172));
#201158=CARTESIAN_POINT('Ctrl Pts',(-20.1163079210326,17.6075930597933,
15.5776268712162));
#201159=CARTESIAN_POINT('Ctrl Pts',(-20.1163584605015,17.6076366315982,
15.5776308725179));
#201160=CARTESIAN_POINT('Ctrl Pts',(-20.1220936267825,17.6125815873703,
15.5780849658487));
#201161=CARTESIAN_POINT('Ctrl Pts',(-20.1277520904035,17.6175131168468,
15.578536307123));
#201162=CARTESIAN_POINT('Ctrl Pts',(-20.1436480051138,17.6315163496052,
15.5798137194793));
#201163=CARTESIAN_POINT('Ctrl Pts',(-20.1538237905432,17.6406572061432,
15.5806426799479));
#201164=CARTESIAN_POINT('Ctrl Pts',(-20.1765018938493,17.6614294584153,
15.5825158773276));
#201165=CARTESIAN_POINT('Ctrl Pts',(-20.1889533862617,17.6731147005853,
15.5835623715763));
#201166=CARTESIAN_POINT('Ctrl Pts',(-20.2277118941701,17.7103800883509,
15.5868777327349));
#201167=CARTESIAN_POINT('Ctrl Pts',(-20.2534949126171,17.7364932023779,
15.5891691783209));
#201168=CARTESIAN_POINT('Ctrl Pts',(-20.3343603276755,17.8227681462414,
15.596640886085));
#201169=CARTESIAN_POINT('Ctrl Pts',(-20.3866450157547,17.8854423435923,
15.6019238840865));
#201170=CARTESIAN_POINT('Ctrl Pts',(-20.4659357021339,17.992493632953,15.610667890851));
#201171=CARTESIAN_POINT('Ctrl Pts',(-20.4951598696652,18.0351280754042,
15.6140835312532));
#201172=CARTESIAN_POINT('Ctrl Pts',(-20.5894724938202,18.1841336649876,
15.6257362678925));
#201173=CARTESIAN_POINT('Ctrl Pts',(-20.6467221531686,18.295175949557,15.6339580316536));
#201174=CARTESIAN_POINT('Ctrl Pts',(-20.6974296624091,18.4193424496933,
15.6422406085192));
#201175=CARTESIAN_POINT('Ctrl Pts',(-20.7009325326663,18.4280861250016,
15.6428191325325));
#201176=CARTESIAN_POINT('Ctrl Pts',(-20.7060465160105,18.441102355905,15.6436730383389));
#201177=CARTESIAN_POINT('Ctrl Pts',(-20.7077022970713,18.4453570759616,
15.643951007541));
#201178=CARTESIAN_POINT('Ctrl Pts',(-20.7106284105698,18.4529486335987,
15.6444448820955));
#201179=CARTESIAN_POINT('Ctrl Pts',(-20.7119040751706,18.4562833527452,
15.644661103868));
#201180=CARTESIAN_POINT('Ctrl Pts',(-20.7146337326333,18.4634734157778,
15.6451257453601));
#201181=CARTESIAN_POINT('Ctrl Pts',(-20.7160849040996,18.4673297702814,
15.6453739957509));
#201182=CARTESIAN_POINT('Ctrl Pts',(-20.7200717134144,18.4780189191715,
15.64605951838));
#201183=CARTESIAN_POINT('Ctrl Pts',(-20.722583368006,18.4848606830103,15.646495381068));
#201184=CARTESIAN_POINT('Ctrl Pts',(-20.7363485352009,18.5229641947135,
15.648907340079));
#201185=CARTESIAN_POINT('Ctrl Pts',(-20.7469008883667,18.5544764152931,
15.6508443529585));
#201186=CARTESIAN_POINT('Ctrl Pts',(-20.8045488109645,18.7411117093909,
15.6620513335706));
#201187=CARTESIAN_POINT('Ctrl Pts',(-20.8344466713562,18.9009955576402,
15.670620709863));
#201188=CARTESIAN_POINT('Ctrl Pts',(-20.8492352643372,19.1116419049396,
15.6821816623415));
#201189=CARTESIAN_POINT('Ctrl Pts',(-20.8509686689526,19.160646635248,15.6848867256134));
#201190=CARTESIAN_POINT('Ctrl Pts',(-20.8509995791044,19.2096650574301,
15.6876314267646));
#201191=CARTESIAN_POINT('Ctrl Pts',(-20.8509995807897,19.2096677326801,
15.6876315765606));
#201192=CARTESIAN_POINT('Ctrl Pts',(-20.8510434871719,19.27943585758,15.6915381231541));
#201193=CARTESIAN_POINT('Ctrl Pts',(-20.8476384984025,19.3491589547705,
15.6955220276476));
#201194=CARTESIAN_POINT('Ctrl Pts',(-20.8397857342339,19.4288578015771,
15.7002212838235));
#201195=CARTESIAN_POINT('Ctrl Pts',(-20.838698304264,19.4391241385988,15.700829353884));
#201196=CARTESIAN_POINT('Ctrl Pts',(-20.8367354837038,19.4564445058437,
15.7018600347468));
#201197=CARTESIAN_POINT('Ctrl Pts',(-20.8358995712248,19.4635028920424,
15.7022814067909));
#201198=CARTESIAN_POINT('Ctrl Pts',(-20.8342941197586,19.4764984975953,
15.7030597630742));
#201199=CARTESIAN_POINT('Ctrl Pts',(-20.8335349079559,19.4824369371732,
15.7034164189799));
#201200=CARTESIAN_POINT('Ctrl Pts',(-20.8319155539216,19.4946898673831,
15.7041543748108));
#201201=CARTESIAN_POINT('Ctrl Pts',(-20.8310520687409,19.5010038480021,
15.7045357768828));
#201202=CARTESIAN_POINT('Ctrl Pts',(-20.8290496276841,19.5151693620982,
15.7053940391335));
#201203=CARTESIAN_POINT('Ctrl Pts',(-20.8278950218306,19.5230185542208,
15.7058713901581));
#201204=CARTESIAN_POINT('Ctrl Pts',(-20.824844961801,19.5429736274424,15.7070895838323));
#201205=CARTESIAN_POINT('Ctrl Pts',(-20.8228884926196,19.555069759064,15.7078323501742));
#201206=CARTESIAN_POINT('Ctrl Pts',(-20.8108297191291,19.6257273900897,
15.71219705076));
#201207=CARTESIAN_POINT('Ctrl Pts',(-20.7983710488112,19.6838546950599,
15.7158933385397));
#201208=CARTESIAN_POINT('Ctrl Pts',(-20.7680792322583,19.8009084968002,
15.7235578177454));
#201209=CARTESIAN_POINT('Ctrl Pts',(-20.7500878968257,19.8597364512723,
15.7275274295434));
#201210=CARTESIAN_POINT('Ctrl Pts',(-20.7272668328434,19.9241785542234,
15.7319934520378));
#201211=CARTESIAN_POINT('Ctrl Pts',(-20.7249393016113,19.9306506018069,
15.7324433106561));
#201212=CARTESIAN_POINT('Ctrl Pts',(-20.7225806013824,19.9371103165536,
15.7328936098053));
#201213=CARTESIAN_POINT('Origin',(-18.734,19.211,0.));
#201214=CARTESIAN_POINT('',(-20.7225806782305,19.9371101060915,16.7554729098499));
#201215=CARTESIAN_POINT('',(-20.7225806064499,19.9371103026755,16.5356516909487));
#201216=CARTESIAN_POINT('',(-20.7225806064498,19.9371103026755,0.));
#201217=CARTESIAN_POINT('Ctrl Pts',(-20.7225806782305,19.9371101060915,
16.7554729098499));
#201218=CARTESIAN_POINT('Ctrl Pts',(-20.7433303988069,19.8802833341313,
16.752186960848));
#201219=CARTESIAN_POINT('Ctrl Pts',(-20.7616463830241,19.8225613684717,
16.7488940370088));
#201220=CARTESIAN_POINT('Ctrl Pts',(-20.8031161608804,19.6693480182463,
16.7401351003016));
#201221=CARTESIAN_POINT('Ctrl Pts',(-20.8221382522373,19.5729387717263,
16.7345998955843));
#201222=CARTESIAN_POINT('Ctrl Pts',(-20.8362368147881,19.4610092278057,
16.727981283592));
#201223=CARTESIAN_POINT('Ctrl Pts',(-20.837918883443,19.446434821374,16.727115946789));
#201224=CARTESIAN_POINT('Ctrl Pts',(-20.8402567481903,19.4241464763026,
16.7257867843257));
#201225=CARTESIAN_POINT('Ctrl Pts',(-20.8410219631865,19.4164442841063,
16.7253264065544));
#201226=CARTESIAN_POINT('Ctrl Pts',(-20.8422815026815,19.4030185085638,
16.7245220094128));
#201227=CARTESIAN_POINT('Ctrl Pts',(-20.8427948028074,19.3972967547408,
16.7241785912338));
#201228=CARTESIAN_POINT('Ctrl Pts',(-20.8438966146394,19.3844264218433,
16.723404731499));
#201229=CARTESIAN_POINT('Ctrl Pts',(-20.8444720950485,19.3772768243325,
16.722973884264));
#201230=CARTESIAN_POINT('Ctrl Pts',(-20.8459169690324,19.3581085313088,
16.7218161322066));
#201231=CARTESIAN_POINT('Ctrl Pts',(-20.8467200885365,19.3460852403305,
16.7210871558742));
#201232=CARTESIAN_POINT('Ctrl Pts',(-20.8498276623789,19.292714307534,16.7178385212459));
#201233=CARTESIAN_POINT('Ctrl Pts',(-20.8510211083857,19.251313432386,16.7152843495757));
#201234=CARTESIAN_POINT('Ctrl Pts',(-20.8509121657265,19.0404276617498,
16.7020917268623));
#201235=CARTESIAN_POINT('Ctrl Pts',(-20.8304727774874,18.8715948023031,
16.6908605528484));
#201236=CARTESIAN_POINT('Ctrl Pts',(-20.7654397441084,18.6062621605717,
16.6728475888321));
#201237=CARTESIAN_POINT('Ctrl Pts',(-20.7333602027718,18.5074240000789,
16.6660710362922));
#201238=CARTESIAN_POINT('Ctrl Pts',(-20.6904971182236,18.4023580057636,
16.6590602461371));
#201239=CARTESIAN_POINT('Ctrl Pts',(-20.6867761548128,18.393413218159,16.6584650174247));
#201240=CARTESIAN_POINT('Ctrl Pts',(-20.6811908871083,18.3802425289996,
16.6575913355819));
#201241=CARTESIAN_POINT('Ctrl Pts',(-20.6793740071344,18.3759968264975,
16.6573101212883));
#201242=CARTESIAN_POINT('Ctrl Pts',(-20.6761257889718,18.3684745083542,
16.6568126810397));
#201243=CARTESIAN_POINT('Ctrl Pts',(-20.6747000297379,18.365195542979,16.6565961206751));
#201244=CARTESIAN_POINT('Ctrl Pts',(-20.6716271656546,18.3581772389677,
16.6561331897535));
#201245=CARTESIAN_POINT('Ctrl Pts',(-20.6699775452151,18.3544390623605,
16.6558869757115));
#201246=CARTESIAN_POINT('Ctrl Pts',(-20.6654189066792,18.3441892537405,
16.6552127965581));
#201247=CARTESIAN_POINT('Ctrl Pts',(-20.6624877595267,18.337687439939,16.654786165289));
#201248=CARTESIAN_POINT('Ctrl Pts',(-20.6466515873257,18.303028492705,16.6525167802173));
#201249=CARTESIAN_POINT('Ctrl Pts',(-20.6331619195366,18.2751407242402,
16.6507078725077));
#201250=CARTESIAN_POINT('Ctrl Pts',(-20.5446480139625,18.1019550982788,
16.6395212216256));
#201251=CARTESIAN_POINT('Ctrl Pts',(-20.4536052251808,17.9654491021103,
16.6308787033376));
#201252=CARTESIAN_POINT('Ctrl Pts',(-20.2715338455183,17.7510196113438,
16.6154835645376));
#201253=CARTESIAN_POINT('Ctrl Pts',(-20.1879783827937,17.6677908194968,
16.6089133162354));
#201254=CARTESIAN_POINT('Ctrl Pts',(-20.0870076699515,17.5827298209735,
16.6011789972353));
#201255=CARTESIAN_POINT('Ctrl Pts',(-20.0759772281774,17.5736269102728,
16.6003368197567));
#201256=CARTESIAN_POINT('Ctrl Pts',(-20.0582778850036,17.5593194552579,
16.5989893686737));
#201257=CARTESIAN_POINT('Ctrl Pts',(-20.0516684382339,17.5540418163682,
16.5984870422964));
#201258=CARTESIAN_POINT('Ctrl Pts',(-20.0399575017301,17.5448050229905,
16.597598401787));
#201259=CARTESIAN_POINT('Ctrl Pts',(-20.0348691627238,17.5408293147749,
16.5972127547795));
#201260=CARTESIAN_POINT('Ctrl Pts',(-20.0243087484434,17.5326556074793,
16.5964132892473));
#201261=CARTESIAN_POINT('Ctrl Pts',(-20.0188341947642,17.5284609495086,
16.595999344932));
#201262=CARTESIAN_POINT('Ctrl Pts',(-20.0047322471532,17.5177648550862,
16.5949342881041));
#201263=CARTESIAN_POINT('Ctrl Pts',(-19.9960754873648,17.5113026277173,
16.5942816486013));
#201264=CARTESIAN_POINT('Ctrl Pts',(-19.9597641716323,17.4846267628509,
16.5915486534249));
#201265=CARTESIAN_POINT('Ctrl Pts',(-19.9316717847602,17.4650204929477,
16.5894450317506));
#201266=CARTESIAN_POINT('Ctrl Pts',(-19.8572711946517,17.4157353899253,
16.5838980747622));
#201267=CARTESIAN_POINT('Ctrl Pts',(-19.810262510711,17.3871657452674,16.5804164834749));
#201268=CARTESIAN_POINT('Ctrl Pts',(-19.6666535097936,17.3073736265223,
16.5698575039541));
#201269=CARTESIAN_POINT('Ctrl Pts',(-19.5671476058028,17.2617700141565,
16.5626316901323));
#201270=CARTESIAN_POINT('Ctrl Pts',(-19.4286066135071,17.2108301809486,
16.5528808362129));
#201271=CARTESIAN_POINT('Ctrl Pts',(-19.3922848272826,17.1985838306067,
16.5503531180982));
#201272=CARTESIAN_POINT('Ctrl Pts',(-19.3246523566846,17.1778078486303,
16.5457178378031));
#201273=CARTESIAN_POINT('Ctrl Pts',(-19.2934388464731,17.168998812263,16.5436060819469));
#201274=CARTESIAN_POINT('Ctrl Pts',(-19.2559593469489,17.1593453522932,
16.5411116142823));
#201275=CARTESIAN_POINT('Ctrl Pts',(-19.2498774174387,17.1578076454257,
16.5407081151772));
#201276=CARTESIAN_POINT('Ctrl Pts',(-19.2015705670124,17.1458223191853,
16.5375138893784));
#201277=CARTESIAN_POINT('Ctrl Pts',(-19.159036170376,17.1366504776844,16.5347656058128));
#201278=CARTESIAN_POINT('Ctrl Pts',(-19.1088550281401,17.1274383430344,
16.5316212389089));
#201279=CARTESIAN_POINT('Ctrl Pts',(-19.1014565557184,17.1261208298778,
16.5311601309494));
#201280=CARTESIAN_POINT('Ctrl Pts',(-19.0894933795238,17.1240560983347,
16.5304187089213));
#201281=CARTESIAN_POINT('Ctrl Pts',(-19.0849330437054,17.1232844084129,
16.5301370597121));
#201282=CARTESIAN_POINT('Ctrl Pts',(-19.0768421071341,17.1219425380944,
16.5296391383916));
#201283=CARTESIAN_POINT('Ctrl Pts',(-19.0733125568911,17.1213663529253,
16.5294225294626));
#201284=CARTESIAN_POINT('Ctrl Pts',(-19.0657516382568,17.1201517249532,
16.5289598131345));
#201285=CARTESIAN_POINT('Ctrl Pts',(-19.0617198897548,17.1195159973696,
16.5287138605878));
#201286=CARTESIAN_POINT('Ctrl Pts',(-19.0506580944794,17.1178045411081,
16.5280411349471));
#201287=CARTESIAN_POINT('Ctrl Pts',(-19.0436243517688,17.1167525595132,
16.5276156861279));
#201288=CARTESIAN_POINT('Ctrl Pts',(-19.0062028345062,17.111348370723,16.5253638122664));
#201289=CARTESIAN_POINT('Ctrl Pts',(-18.975726688986,17.1076218177237,16.523570617579));
#201290=CARTESIAN_POINT('Ctrl Pts',(-18.8834965209076,17.0983754002523,
16.518237592611));
#201291=CARTESIAN_POINT('Ctrl Pts',(-18.8215679796411,17.0949033867494,
16.5147825375925));
#201292=CARTESIAN_POINT('Ctrl Pts',(-18.612811185808,17.0923815271823,16.5033037353659));
#201293=CARTESIAN_POINT('Ctrl Pts',(-18.4662667659925,17.1058751584313,
16.4954967731419));
#201294=CARTESIAN_POINT('Ctrl Pts',(-18.2488474790931,17.1489809438541,
16.4831218539245));
#201295=CARTESIAN_POINT('Ctrl Pts',(-18.1762313567562,17.1674276533659,
16.478855777376));
#201296=CARTESIAN_POINT('Ctrl Pts',(-18.0922192294708,17.1935811851993,
16.4736930223595));
#201297=CARTESIAN_POINT('Ctrl Pts',(-18.0797254235962,17.1975984010081,
16.4729192958104));
#201298=CARTESIAN_POINT('Ctrl Pts',(-18.0594877861536,17.2043138002028,
16.4716559650957));
#201299=CARTESIAN_POINT('Ctrl Pts',(-18.0517207433681,17.2069413072056,
16.4711686904058));
#201300=CARTESIAN_POINT('Ctrl Pts',(-18.0379186543715,17.2116999420527,
16.4702984058485));
#201301=CARTESIAN_POINT('Ctrl Pts',(-18.031877608758,17.2138134519362,16.4699159839097));
#201302=CARTESIAN_POINT('Ctrl Pts',(-18.0191704131458,17.2183239489796,
16.4691083492976));
#201303=CARTESIAN_POINT('Ctrl Pts',(-18.0125065358845,17.2207270634679,
16.4686829364463));
#201304=CARTESIAN_POINT('Ctrl Pts',(-17.9949161869802,17.2271704136063,
16.4675549638021));
#201305=CARTESIAN_POINT('Ctrl Pts',(-17.9840109017698,17.2312674285262,
16.4668505144229));
#201306=CARTESIAN_POINT('Ctrl Pts',(-17.9335448902501,17.2507038603733,
16.4635661609879));
#201307=CARTESIAN_POINT('Ctrl Pts',(-17.8944194871903,17.267139538666,16.4609496343936));
#201308=CARTESIAN_POINT('Ctrl Pts',(-17.7880576170252,17.3156299758322,
16.4536357557298));
#201309=CARTESIAN_POINT('Ctrl Pts',(-17.72198239082,17.3500720048569,16.4488625503694));
#201310=CARTESIAN_POINT('Ctrl Pts',(-17.5421294548141,17.4562364227782,
16.4352579366508));
#201311=CARTESIAN_POINT('Ctrl Pts',(-17.4331691595399,17.5354142354494,
16.426265373199));
#201312=CARTESIAN_POINT('Ctrl Pts',(-17.3217701230268,17.633819317249,16.4165947511318));
#201313=CARTESIAN_POINT('Ctrl Pts',(-17.3111838170296,17.643362843451,16.4156707861006));
#201314=CARTESIAN_POINT('Ctrl Pts',(-17.2944109768497,17.6587933952721,
16.4141998638855));
#201315=CARTESIAN_POINT('Ctrl Pts',(-17.2881623843253,17.6646121146778,
16.4136502980441));
#201316=CARTESIAN_POINT('Ctrl Pts',(-17.2503901483772,17.7002148992286,
16.4103193771155));
#201317=CARTESIAN_POINT('Ctrl Pts',(-17.2197501394194,17.7309264323014,
16.4075795233403));
#201318=CARTESIAN_POINT('Ctrl Pts',(-17.1849360626935,17.7680355895156,
16.4044436079217));
#201319=CARTESIAN_POINT('Ctrl Pts',(-17.1798281289161,17.7735386367764,
16.4039829081168));
#201320=CARTESIAN_POINT('Ctrl Pts',(-17.1716224247503,17.7824739464397,
16.4032420129867));
#201321=CARTESIAN_POINT('Ctrl Pts',(-17.1685064836133,17.7858893290587,
16.4029604855227));
#201322=CARTESIAN_POINT('Ctrl Pts',(-17.1630002078915,17.7919646088739,
16.4024626989407));
#201323=CARTESIAN_POINT('Ctrl Pts',(-17.1606054017412,17.7946203803622,
16.4022461036791));
#201324=CARTESIAN_POINT('Ctrl Pts',(-17.1554908540555,17.8003212467121,
16.4017833276159));
#201325=CARTESIAN_POINT('Ctrl Pts',(-17.152773195974,17.8033681363064,16.401537302131));
#201326=CARTESIAN_POINT('Ctrl Pts',(-17.1453421272597,17.8117481210668,
16.400864171133));
#201327=CARTESIAN_POINT('Ctrl Pts',(-17.1406467204629,17.8170972102824,
16.4004383925599));
#201328=CARTESIAN_POINT('Ctrl Pts',(-17.1157935924048,17.845700003754,16.398181651692));
#201329=CARTESIAN_POINT('Ctrl Pts',(-17.0961166088964,17.8693687993891,
16.3963840902856));
#201330=CARTESIAN_POINT('Ctrl Pts',(-17.0382313230102,17.9421697107767,
16.3910333186897));
#201331=CARTESIAN_POINT('Ctrl Pts',(-17.0016647670121,17.9925676145352,
16.3875655490246));
#201332=CARTESIAN_POINT('Ctrl Pts',(-16.8863177412652,18.1672583560864,
16.3760574297048));
#201333=CARTESIAN_POINT('Ctrl Pts',(-16.818281524111,18.2981200823489,16.3682331100459));
#201334=CARTESIAN_POINT('Ctrl Pts',(-16.7371336029532,18.5040839523418,
16.3558692723939));
#201335=CARTESIAN_POINT('Ctrl Pts',(-16.7135651951433,18.5745668284206,
16.3516362908328));
#201336=CARTESIAN_POINT('Ctrl Pts',(-16.6902553974999,18.6587604200131,
16.3465102075234));
#201337=CARTESIAN_POINT('Ctrl Pts',(-16.6868778808701,18.6714153710422,
16.3457379844783));
#201338=CARTESIAN_POINT('Ctrl Pts',(-16.681579254526,18.6920345035618,16.3444766272564));
#201339=CARTESIAN_POINT('Ctrl Pts',(-16.6795865296114,18.6999800466228,
16.3439898104134));
#201340=CARTESIAN_POINT('Ctrl Pts',(-16.6761193534797,18.7141527456894,
16.3431200382777));
#201341=CARTESIAN_POINT('Ctrl Pts',(-16.6746269208013,18.7203754299656,
16.342737668335));
#201342=CARTESIAN_POINT('Ctrl Pts',(-16.6715408694223,18.733504892844,16.341929827623));
#201343=CARTESIAN_POINT('Ctrl Pts',(-16.6699536828267,18.7404130884501,
16.3415041550758));
#201344=CARTESIAN_POINT('Ctrl Pts',(-16.6658455440473,18.7587143570004,
16.3403747603357));
#201345=CARTESIAN_POINT('Ctrl Pts',(-16.6633840695393,18.7701204058692,
16.3396691400229));
#201346=CARTESIAN_POINT('Ctrl Pts',(-16.6523679079481,18.8232956412068,
16.3363710424774));
#201347=CARTESIAN_POINT('Ctrl Pts',(-16.6449825124726,18.8652944023139,
16.3337415680137));
#201348=CARTESIAN_POINT('Ctrl Pts',(-16.6281179436273,18.9817086935717,
16.326380479851));
#201349=CARTESIAN_POINT('Ctrl Pts',(-16.6213182247392,19.0564440453024,
16.3215718017951));
#201350=CARTESIAN_POINT('Ctrl Pts',(-16.6120664102933,19.3022537914196,
16.3055433579993));
#201351=CARTESIAN_POINT('Ctrl Pts',(-16.6263613065639,19.4732734475288,
16.2940036296611));
#201352=CARTESIAN_POINT('Ctrl Pts',(-16.6672423124823,19.6704849154768,
16.2812247042703));
#201353=CARTESIAN_POINT('Ctrl Pts',(-16.674056033928,19.7001265730077,16.2793203808293));
#201354=CARTESIAN_POINT('Ctrl Pts',(-16.6833085988988,19.7367450849189,
16.2769968315207));
#201355=CARTESIAN_POINT('Ctrl Pts',(-16.6851479341194,19.7438680255511,
16.276546235937));
#201356=CARTESIAN_POINT('Ctrl Pts',(-16.688090485319,19.7550227265425,16.2758429095609));
#201357=CARTESIAN_POINT('Ctrl Pts',(-16.6891685551354,19.7590609747528,
16.2755887675572));
#201358=CARTESIAN_POINT('Ctrl Pts',(-16.6911880365819,19.766536662922,16.2751192148015));
#201359=CARTESIAN_POINT('Ctrl Pts',(-16.6921261605398,19.7699748883077,
16.2749036228578));
#201360=CARTESIAN_POINT('Ctrl Pts',(-16.6942640504025,19.777733055652,16.274417964383));
#201361=CARTESIAN_POINT('Ctrl Pts',(-16.6954688559691,19.7820515529399,
16.274148194014));
#201362=CARTESIAN_POINT('Ctrl Pts',(-16.6991354261947,19.7950345006919,
16.2733387822597));
#201363=CARTESIAN_POINT('Ctrl Pts',(-16.7016388144918,19.8036872277017,
16.2728015022325));
#201364=CARTESIAN_POINT('Ctrl Pts',(-16.7277644403993,19.891875747321,16.26734524086));
#201365=CARTESIAN_POINT('Ctrl Pts',(-16.7559907964435,19.9699834068524,
16.2626755088247));
#201366=CARTESIAN_POINT('Ctrl Pts',(-16.8485677865108,20.1855942737558,
16.2497330287895));
#201367=CARTESIAN_POINT('Ctrl Pts',(-16.9232019018568,20.3181135927675,
16.2416851553575));
#201368=CARTESIAN_POINT('Ctrl Pts',(-17.0557624904192,20.5036887730365,
16.2289639746873));
#201369=CARTESIAN_POINT('Ctrl Pts',(-17.1034966250975,20.5633987167373,
16.2246145228551));
#201370=CARTESIAN_POINT('Ctrl Pts',(-17.1631304904082,20.6302363970677,
16.2193592460446));
#201371=CARTESIAN_POINT('Ctrl Pts',(-17.1720031448699,20.6399957241842,
16.2185816840114));
#201372=CARTESIAN_POINT('Ctrl Pts',(-17.1865519963965,20.6557010882305,
16.2173133199146));
#201373=CARTESIAN_POINT('Ctrl Pts',(-17.1921727314229,20.6616981867889,
16.216824878432));
#201374=CARTESIAN_POINT('Ctrl Pts',(-17.2022336348675,20.6723082478024,
16.2159532860197));
#201375=CARTESIAN_POINT('Ctrl Pts',(-17.2066600972128,20.6769341091636,
16.2155707295928));
#201376=CARTESIAN_POINT('Ctrl Pts',(-17.2160207792201,20.6866280414095,
16.2147636105943));
#201377=CARTESIAN_POINT('Ctrl Pts',(-17.2209595430058,20.6916915968297,
16.2143388518875));
#201378=CARTESIAN_POINT('Ctrl Pts',(-17.2340654490494,20.7049946228789,
16.2132144611913));
#201379=CARTESIAN_POINT('Ctrl Pts',(-17.2422750200814,20.7131917874288,
16.2125129610422));
#201380=CARTESIAN_POINT('Ctrl Pts',(-17.2804559253733,20.7506933595815,
16.2092629471553));
#201381=CARTESIAN_POINT('Ctrl Pts',(-17.3112243625633,20.779169350315,16.2066787380752));
#201382=CARTESIAN_POINT('Ctrl Pts',(-17.4702251520484,20.9177904566099,
16.1934856211139));
#201383=CARTESIAN_POINT('Ctrl Pts',(-17.6104627465081,21.0131949405217,
16.1822878734906));
#201384=CARTESIAN_POINT('Ctrl Pts',(-17.8533937170849,21.1389940845405,
16.1642470087988));
#201385=CARTESIAN_POINT('Ctrl Pts',(-17.9497204562445,21.1801468752051,
16.1574134825229));
#201386=CARTESIAN_POINT('Ctrl Pts',(-18.0578526454002,21.2171423754431,
16.1503527124055));
#201387=CARTESIAN_POINT('Ctrl Pts',(-18.0670218837612,21.220209465506,16.1497586816396));
#201388=CARTESIAN_POINT('Ctrl Pts',(-18.080597928524,21.2246474430503,16.1488864161077));
#201389=CARTESIAN_POINT('Ctrl Pts',(-18.0849885711777,21.2260668619431,
16.1486054328108));
#201390=CARTESIAN_POINT('Ctrl Pts',(-18.0927892185566,21.2285605357067,
16.1481082477782));
#201391=CARTESIAN_POINT('Ctrl Pts',(-18.0961973347639,21.2296405183625,
16.147891712912));
#201392=CARTESIAN_POINT('Ctrl Pts',(-18.1035086599993,21.2319370065192,
16.1474286666505));
#201393=CARTESIAN_POINT('Ctrl Pts',(-18.1074126508788,21.2331508372785,
16.1471823126587));
#201394=CARTESIAN_POINT('Ctrl Pts',(-18.1181467539414,21.2364542194643,
16.1465073553206));
#201395=CARTESIAN_POINT('Ctrl Pts',(-18.124984035559,21.2385205484021,16.1460800909514));
#201396=CARTESIAN_POINT('Ctrl Pts',(-18.1616683722007,21.24940479267,16.1438012626415));
#201397=CARTESIAN_POINT('Ctrl Pts',(-18.1916983735129,21.257598829291,16.1419838793355));
#201398=CARTESIAN_POINT('Ctrl Pts',(-18.3809297596199,21.3047747632879,
16.1307686751546));
#201399=CARTESIAN_POINT('Ctrl Pts',(-18.5440426464886,21.3258238551038,
16.1221080159552));
#201400=CARTESIAN_POINT('Ctrl Pts',(-18.8251657643572,21.3292813330703,
16.1067187015476));
#201401=CARTESIAN_POINT('Ctrl Pts',(-18.9422677222171,21.3209872657003,
16.1001766564776));
#201402=CARTESIAN_POINT('Ctrl Pts',(-19.0721994938407,21.3008599103215,
16.0924740809648));
#201403=CARTESIAN_POINT('Ctrl Pts',(-19.0863030542917,21.2985286549926,
16.0916322862241));
#201404=CARTESIAN_POINT('Ctrl Pts',(-19.1087102087637,21.2945913144706,
16.0902853331548));
#201405=CARTESIAN_POINT('Ctrl Pts',(-19.1170298087498,21.2930779689371,
16.0897831186065));
#201406=CARTESIAN_POINT('Ctrl Pts',(-19.1316858092682,21.2903212091437,
16.0888946083805));
#201407=CARTESIAN_POINT('Ctrl Pts',(-19.1380260415081,21.2890985660084,
16.0885089792002));
#201408=CARTESIAN_POINT('Ctrl Pts',(-19.1511273017089,21.2865099110984,
16.0877094843103));
#201409=CARTESIAN_POINT('Ctrl Pts',(-19.1578874379376,21.2851398253506,
16.0872954924832));
#201410=CARTESIAN_POINT('Ctrl Pts',(-19.1752210551124,21.2815385185251,
16.0862301737871));
#201411=CARTESIAN_POINT('Ctrl Pts',(-19.1857842702045,21.2792593509,16.0855773184774));
#201412=CARTESIAN_POINT('Ctrl Pts',(-19.2297868470935,21.2694119761867,
16.0828422335204));
#201413=CARTESIAN_POINT('Ctrl Pts',(-19.2630557912861,21.2611132201042,
16.080736693342));
#201414=CARTESIAN_POINT('Ctrl Pts',(-19.3491912086119,21.2373909875361,
16.0751834720756));
#201415=CARTESIAN_POINT('Ctrl Pts',(-19.4016807857419,21.2207069952663,
16.0716974271914));
#201416=CARTESIAN_POINT('Ctrl Pts',(-19.6494098754055,21.1311888175244,
16.0547669633032));
#201417=CARTESIAN_POINT('Ctrl Pts',(-19.8338097655697,21.031853061553,16.0405739686977));
#201418=CARTESIAN_POINT('Ctrl Pts',(-20.00435118889,20.9044926485973,16.0271549253794));
#201419=CARTESIAN_POINT('Ctrl Pts',(-20.0079697057802,20.901772215119,16.0268701185296));
#201420=CARTESIAN_POINT('Ctrl Pts',(-20.0279634473045,20.8866401141797,
16.025296105304));
#201421=CARTESIAN_POINT('Ctrl Pts',(-20.0441667115951,20.8740016402553,
16.0240192156397));
#201422=CARTESIAN_POINT('Ctrl Pts',(-20.0652102920254,20.8570892256756,
16.0223620048336));
#201423=CARTESIAN_POINT('Ctrl Pts',(-20.0702181075084,20.8530267208939,
16.0219677178025));
#201424=CARTESIAN_POINT('Ctrl Pts',(-20.0782511226781,20.8464489889606,
16.0213354907494));
#201425=CARTESIAN_POINT('Ctrl Pts',(-20.081287964225,20.8439481370676,16.0210965377843));
#201426=CARTESIAN_POINT('Ctrl Pts',(-20.0869604319314,20.8392502395933,
16.020650337992));
#201427=CARTESIAN_POINT('Ctrl Pts',(-20.0895976882824,20.837055251444,16.0204429486207));
#201428=CARTESIAN_POINT('Ctrl Pts',(-20.0958336410269,20.831839353648,16.0199526787635));
#201429=CARTESIAN_POINT('Ctrl Pts',(-20.099427661045,20.8288128382458,16.01967020676));
#201430=CARTESIAN_POINT('Ctrl Pts',(-20.1106565996605,20.8192929029103,
16.018787841166));
#201431=CARTESIAN_POINT('Ctrl Pts',(-20.1182556286363,20.8127571034364,
16.0181909641413));
#201432=CARTESIAN_POINT('Ctrl Pts',(-20.1360726278116,20.7972114976654,
16.016791308788));
#201433=CARTESIAN_POINT('Ctrl Pts',(-20.1462507307738,20.788156448322,16.0159915924635));
#201434=CARTESIAN_POINT('Ctrl Pts',(-20.1816416892114,20.7560531975546,
16.0132073665971));
#201435=CARTESIAN_POINT('Ctrl Pts',(-20.2063845877909,20.7324925959874,
16.0112545122457));
#201436=CARTESIAN_POINT('Ctrl Pts',(-20.2842584683261,20.6546600397496,
16.005045449642));
#201437=CARTESIAN_POINT('Ctrl Pts',(-20.3350451785142,20.5981233988142,
16.0008961828023));
#201438=CARTESIAN_POINT('Ctrl Pts',(-20.4906155867975,20.4049823850317,
15.9874090117612));
#201439=CARTESIAN_POINT('Ctrl Pts',(-20.5817953836118,20.2583479078304,
15.978142784349));
#201440=CARTESIAN_POINT('Ctrl Pts',(-20.6640064837358,20.0812319187437,
15.9667988654617));
#201441=CARTESIAN_POINT('Ctrl Pts',(-20.6734389218583,20.0600024883679,
15.9654381553835));
#201442=CARTESIAN_POINT('Ctrl Pts',(-20.6862672065903,20.02980011932,15.9634990949465));
#201443=CARTESIAN_POINT('Ctrl Pts',(-20.6899545521561,20.0209522619473,
15.9629306601334));
#201444=CARTESIAN_POINT('Ctrl Pts',(-20.6958422183918,20.0065499976889,
15.9620046405147));
#201445=CARTESIAN_POINT('Ctrl Pts',(-20.6980793649531,20.0010107187413,
15.9616483063261));
#201446=CARTESIAN_POINT('Ctrl Pts',(-20.7027084833689,19.9894076045086,
15.9609014923674));
#201447=CARTESIAN_POINT('Ctrl Pts',(-20.7050959508037,19.9833420501925,
15.960510865377));
#201448=CARTESIAN_POINT('Ctrl Pts',(-20.7107007408829,19.9689073650376,
15.9595806725925));
#201449=CARTESIAN_POINT('Ctrl Pts',(-20.7138929632435,19.9605286807176,
15.9590402710366));
#201450=CARTESIAN_POINT('Ctrl Pts',(-20.7189003798113,19.9471304031136,
15.9581753084636));
#201451=CARTESIAN_POINT('Ctrl Pts',(-20.7207499860271,19.942123778256,15.9578519123852));
#201452=CARTESIAN_POINT('Ctrl Pts',(-20.7225806064913,19.9371103025619,
15.9575278864865));
#201453=CARTESIAN_POINT('Ctrl Pts',(-20.7225806013824,19.9371103165536,
15.7328936098053));
#201454=CARTESIAN_POINT('Ctrl Pts',(-20.6687684267845,20.0844844057023,
15.743166884953));
#201455=CARTESIAN_POINT('Ctrl Pts',(-20.5987347395985,20.2254367109955,
15.7537162423725));
#201456=CARTESIAN_POINT('Ctrl Pts',(-20.4968362899241,20.3836351557168,
15.7656589472727));
#201457=CARTESIAN_POINT('Ctrl Pts',(-20.4793387436348,20.4095232178004,
15.7676152445733));
#201458=CARTESIAN_POINT('Ctrl Pts',(-20.4571389077526,20.440850577118,15.7699758583636));
#201459=CARTESIAN_POINT('Ctrl Pts',(-20.4529746813286,20.4466642690325,
15.7704136454338));
#201460=CARTESIAN_POINT('Ctrl Pts',(-20.4463824402328,20.4557699015741,
15.7710987177525));
#201461=CARTESIAN_POINT('Ctrl Pts',(-20.4439742522762,20.4590760340178,
15.7713473314855));
#201462=CARTESIAN_POINT('Ctrl Pts',(-20.4394433479387,20.4652586521843,
15.771811979727));
#201463=CARTESIAN_POINT('Ctrl Pts',(-20.4373229518937,20.4681367075116,
15.7720281624065));
#201464=CARTESIAN_POINT('Ctrl Pts',(-20.4324506101249,20.4747150745302,
15.7725220461787));
#201465=CARTESIAN_POINT('Ctrl Pts',(-20.4296938624,20.4784117683572,15.7727994080052));
#201466=CARTESIAN_POINT('Ctrl Pts',(-20.4224404950687,20.4880722295795,
15.7735238561962));
#201467=CARTESIAN_POINT('Ctrl Pts',(-20.417924310188,20.4940213194787,15.7739696100002));
#201468=CARTESIAN_POINT('Ctrl Pts',(-20.3874376245079,20.5337426182823,
15.7769442570205));
#201469=CARTESIAN_POINT('Ctrl Pts',(-20.3604823100834,20.5667506624727,
15.7794084446909));
#201470=CARTESIAN_POINT('Ctrl Pts',(-20.2836442205211,20.6552491803633,
15.7860635771181));
#201471=CARTESIAN_POINT('Ctrl Pts',(-20.2317951831533,20.7089532634295,
15.790158518054));
#201472=CARTESIAN_POINT('Ctrl Pts',(-20.1743796533674,20.7624543133703,
15.7944341890725));
#201473=CARTESIAN_POINT('Ctrl Pts',(-20.1715358442198,20.7650896785448,
15.7946453290362));
#201474=CARTESIAN_POINT('Ctrl Pts',(-20.0884525749971,20.8416599783403,
15.8007958993886));
#201475=CARTESIAN_POINT('Ctrl Pts',(-20.0026247582199,20.9092885662888,
15.8066722015024));
#201476=CARTESIAN_POINT('Ctrl Pts',(-19.8664211878089,21.0005017380355,
15.8157891402054));
#201477=CARTESIAN_POINT('Ctrl Pts',(-19.8197069438152,21.0292227620463,
15.8188809591168));
#201478=CARTESIAN_POINT('Ctrl Pts',(-19.7521462118145,21.0672280859273,
15.823341134852));
#201479=CARTESIAN_POINT('Ctrl Pts',(-19.7321821352076,21.0780395776416,
15.8246576473177));
#201480=CARTESIAN_POINT('Ctrl Pts',(-19.696742059131,21.096501151957,15.8269945800711));
#201481=CARTESIAN_POINT('Ctrl Pts',(-19.6813389625752,21.1042870173958,
15.8280102182647));
#201482=CARTESIAN_POINT('Ctrl Pts',(-19.6584581504781,21.1155035480535,
15.8295195716713));
#201483=CARTESIAN_POINT('Ctrl Pts',(-19.6510526277356,21.1190804782773,
15.830008182365));
#201484=CARTESIAN_POINT('Ctrl Pts',(-19.6381021944432,21.1252428399773,
15.8308628926934));
#201485=CARTESIAN_POINT('Ctrl Pts',(-19.6325665357398,21.1278475703709,
15.8312283175899));
#201486=CARTESIAN_POINT('Ctrl Pts',(-19.6215183369507,21.1329877777601,
15.8319578322705));
#201487=CARTESIAN_POINT('Ctrl Pts',(-19.6160060317938,21.1355236228662,
15.8323219049781));
#201488=CARTESIAN_POINT('Ctrl Pts',(-19.6028189278206,21.1415215769473,
15.8331931371012));
#201489=CARTESIAN_POINT('Ctrl Pts',(-19.5951342713639,21.1449616469509,
15.8337010485587));
#201490=CARTESIAN_POINT('Ctrl Pts',(-19.5674262336606,21.1571673833539,
15.8355332667941));
#201491=CARTESIAN_POINT('Ctrl Pts',(-19.5472884310441,21.1656684226986,
15.8368665538985));
#201492=CARTESIAN_POINT('Ctrl Pts',(-19.3527347733059,21.2442710151523,
15.8497675630087));
#201493=CARTESIAN_POINT('Ctrl Pts',(-19.1698748073467,21.2911462019796,
15.8621583631002));
#201494=CARTESIAN_POINT('Ctrl Pts',(-18.9052259702644,21.3225277001215,
15.8797490960574));
#201495=CARTESIAN_POINT('Ctrl Pts',(-18.8267085652016,21.3274296231783,
15.8849098323942));
#201496=CARTESIAN_POINT('Ctrl Pts',(-18.7124858595279,21.3281901831663,
15.892188560959));
#201497=CARTESIAN_POINT('Ctrl Pts',(-18.6768730135779,21.3275287581502,
15.8944252552227));
#201498=CARTESIAN_POINT('Ctrl Pts',(-18.6338579301177,21.3256432157692,
15.897074039299));
#201499=CARTESIAN_POINT('Ctrl Pts',(-18.6264260007521,21.3252781753177,
15.8975297716938));
#201500=CARTESIAN_POINT('Ctrl Pts',(-18.6148484321837,21.3246483050234,
15.8982365772241));
#201501=CARTESIAN_POINT('Ctrl Pts',(-18.6107014713951,21.324410449243,15.8984891190385));
#201502=CARTESIAN_POINT('Ctrl Pts',(-18.6029952415105,21.3239456861523,
15.8989572114241));
#201503=CARTESIAN_POINT('Ctrl Pts',(-18.5994358801478,21.3237219924297,
15.8991729337287));
#201504=CARTESIAN_POINT('Ctrl Pts',(-18.5913686625607,21.323194525544,15.8996607878753));
#201505=CARTESIAN_POINT('Ctrl Pts',(-18.5868612146184,21.322885316693,15.8999326118657));
#201506=CARTESIAN_POINT('Ctrl Pts',(-18.5752126903372,21.3220487588623,
15.9006332019892));
#201507=CARTESIAN_POINT('Ctrl Pts',(-18.5680731709321,21.3214996002596,
15.9010607746325));
#201508=CARTESIAN_POINT('Ctrl Pts',(-18.5239705186385,21.3178821256638,
15.9036914580934));
#201509=CARTESIAN_POINT('Ctrl Pts',(-18.4870880847228,21.3138788733836,
15.9058456942657));
#201510=CARTESIAN_POINT('Ctrl Pts',(-18.2814941211887,21.2860791065581,
15.9176916625751));
#201511=CARTESIAN_POINT('Ctrl Pts',(-18.1160191661373,21.2429514013927,
15.926655953448));
#201512=CARTESIAN_POINT('Ctrl Pts',(-17.8690123270759,21.1455621848431,
15.9412632235049));
#201513=CARTESIAN_POINT('Ctrl Pts',(-17.782994299292,21.1047580696582,15.9465966981626));
#201514=CARTESIAN_POINT('Ctrl Pts',(-17.6813795596371,21.0478819636713,
15.9533777694065));
#201515=CARTESIAN_POINT('Ctrl Pts',(-17.6629023211226,21.0371694480811,
15.9546309936433));
#201516=CARTESIAN_POINT('Ctrl Pts',(-17.6368704666303,21.0215460114992,
15.9564269250107));
#201517=CARTESIAN_POINT('Ctrl Pts',(-17.6291798633218,21.0168633764833,
15.9569613196871));
#201518=CARTESIAN_POINT('Ctrl Pts',(-17.6159677045651,21.0087028027055,
15.9578861102114));
#201519=CARTESIAN_POINT('Ctrl Pts',(-17.6104318863239,21.005248107969,15.9582756468334));
#201520=CARTESIAN_POINT('Ctrl Pts',(-17.5998655155545,20.9985859600986,
15.95902315031));
#201521=CARTESIAN_POINT('Ctrl Pts',(-17.5948323690298,20.9953827226711,
15.9593809582131));
#201522=CARTESIAN_POINT('Ctrl Pts',(-17.5817849385572,20.9870012653827,
15.9603130885546));
#201523=CARTESIAN_POINT('Ctrl Pts',(-17.5737920692595,20.9817901047953,
15.9608886367991));
#201524=CARTESIAN_POINT('Ctrl Pts',(-17.5466837792203,20.9638538205662,
15.9628562958938));
#201525=CARTESIAN_POINT('Ctrl Pts',(-17.5277408188304,20.9508721352653,
15.9642580285542));
#201526=CARTESIAN_POINT('Ctrl Pts',(-17.3655555694147,20.8358041045491,
15.9764977884836));
#201527=CARTESIAN_POINT('Ctrl Pts',(-17.2353678326145,20.7165585569388,
15.9880431994529));
#201528=CARTESIAN_POINT('Ctrl Pts',(-17.0652545836154,20.5165647747321,
16.0053902667699));
#201529=CARTESIAN_POINT('Ctrl Pts',(-17.013171935578,20.4471081377049,16.0111054114842));
#201530=CARTESIAN_POINT('Ctrl Pts',(-16.9447441029803,20.343111946813,16.019053011665));
#201531=CARTESIAN_POINT('Ctrl Pts',(-16.9248393865284,20.3110238214218,
16.0214275260871));
#201532=CARTESIAN_POINT('Ctrl Pts',(-16.9019865256411,20.2718830748952,
16.0242165390101));
#201533=CARTESIAN_POINT('Ctrl Pts',(-16.8982058398658,20.265327308961,16.0246801364237));
#201534=CARTESIAN_POINT('Ctrl Pts',(-16.8923908775128,20.2551179644544,
16.0253964507646));
#201535=CARTESIAN_POINT('Ctrl Pts',(-16.890332178726,20.2514784712916,16.0256506996772));
#201536=CARTESIAN_POINT('Ctrl Pts',(-16.886538829989,20.2447257498905,16.0261203510784));
#201537=CARTESIAN_POINT('Ctrl Pts',(-16.8848012731718,20.2416142681333,
16.0263359353877));
#201538=CARTESIAN_POINT('Ctrl Pts',(-16.8808966112612,20.2345804369597,
16.0268214520563));
#201539=CARTESIAN_POINT('Ctrl Pts',(-16.8787341040025,20.2306555968949,
16.027091089014));
#201540=CARTESIAN_POINT('Ctrl Pts',(-16.8724048309785,20.2190814940319,
16.0278825614101));
#201541=CARTESIAN_POINT('Ctrl Pts',(-16.8682727352556,20.2114132403275,
16.0284022381136));
#201542=CARTESIAN_POINT('Ctrl Pts',(-16.8392494380522,20.1567471374626,
16.0320752168742));
#201543=CARTESIAN_POINT('Ctrl Pts',(-16.8160874659028,20.1088473493953,
16.0351277602357));
#201544=CARTESIAN_POINT('Ctrl Pts',(-16.7881148402491,20.0449627115505,
16.0390503640187));
#201545=CARTESIAN_POINT('Ctrl Pts',(-16.7816550682472,20.0297259289341,
16.0399751236528));
#201546=CARTESIAN_POINT('Ctrl Pts',(-16.7187558543483,19.8763854384308,
16.049188503332));
#201547=CARTESIAN_POINT('Ctrl Pts',(-16.676885167547,19.7327555678079,16.0570959370483));
#201548=CARTESIAN_POINT('Ctrl Pts',(-16.6395509025466,19.5252737510594,
16.0687600125105));
#201549=CARTESIAN_POINT('Ctrl Pts',(-16.6312927524878,19.4641923995311,
16.0722178001693));
#201550=CARTESIAN_POINT('Ctrl Pts',(-16.6223414882622,19.3658199989051,
16.0778869035785));
#201551=CARTESIAN_POINT('Ctrl Pts',(-16.6199486744876,19.3287185087264,
16.080047418603));
#201552=CARTESIAN_POINT('Ctrl Pts',(-16.6181104691525,19.2804570243006,
16.0828944109975));
#201553=CARTESIAN_POINT('Ctrl Pts',(-16.6177746661088,19.2693362153922,
16.0835529452572));
#201554=CARTESIAN_POINT('Ctrl Pts',(-16.617371142953,19.2512471679603,16.0846283839078));
#201555=CARTESIAN_POINT('Ctrl Pts',(-16.6172501383691,19.2442802421015,
16.0850436143827));
#201556=CARTESIAN_POINT('Ctrl Pts',(-16.6170835927895,19.2308818848883,
16.0858441892655));
#201557=CARTESIAN_POINT('Ctrl Pts',(-16.6170329608621,19.2244505855536,
16.086229369544));
#201558=CARTESIAN_POINT('Ctrl Pts',(-16.6169841377642,19.2097255763105,
16.087113373366));
#201559=CARTESIAN_POINT('Ctrl Pts',(-16.6170053768579,19.2014319466948,
16.0876128005249));
#201560=CARTESIAN_POINT('Ctrl Pts',(-16.6171912595583,19.1794010358939,
16.0889436078002));
#201561=CARTESIAN_POINT('Ctrl Pts',(-16.6174408901145,19.1656650406568,
16.0897776345287));
#201562=CARTESIAN_POINT('Ctrl Pts',(-16.6203596092514,19.0610974959766,
16.096160397941));
#201563=CARTESIAN_POINT('Ctrl Pts',(-16.6287404576868,18.9705318584629,
16.1018878466984));
#201564=CARTESIAN_POINT('Ctrl Pts',(-16.6648429900671,18.7419059894704,
16.1168361282648));
#201565=CARTESIAN_POINT('Ctrl Pts',(-16.7005575127879,18.6055525266388,
16.1262342150391));
#201566=CARTESIAN_POINT('Ctrl Pts',(-16.7683400732216,18.4230969446966,
16.1389735316258));
#201567=CARTESIAN_POINT('Ctrl Pts',(-16.7890967542797,18.373168075765,16.1424735128415));
#201568=CARTESIAN_POINT('Ctrl Pts',(-16.8234970298246,18.2986105420742,
16.1476683327111));
#201569=CARTESIAN_POINT('Ctrl Pts',(-16.8357568570056,18.2733703987011,
16.1494211408575));
#201570=CARTESIAN_POINT('Ctrl Pts',(-16.851657273664,18.2422262384442,16.1515698932825));
#201571=CARTESIAN_POINT('Ctrl Pts',(-16.8548292236553,18.236087728643,16.1519927197007));
#201572=CARTESIAN_POINT('Ctrl Pts',(-16.8599018662612,18.226387649803,16.1526596385724));
#201573=CARTESIAN_POINT('Ctrl Pts',(-16.8617827574412,18.2228158611174,
16.1529049471288));
#201574=CARTESIAN_POINT('Ctrl Pts',(-16.8653533343664,18.2160821686095,
16.1533668788016));
#201575=CARTESIAN_POINT('Ctrl Pts',(-16.8670408141831,18.2129192162611,
16.1535836298079));
#201576=CARTESIAN_POINT('Ctrl Pts',(-16.8709224294182,18.2056879436735,
16.1540786747053));
#201577=CARTESIAN_POINT('Ctrl Pts',(-16.8731218573104,18.2016225168015,
16.1543566284197));
#201578=CARTESIAN_POINT('Ctrl Pts',(-16.879007174615,18.1908287038242,16.1550937284313));
#201579=CARTESIAN_POINT('Ctrl Pts',(-16.8827163919936,18.1841130234875,
16.1555514292739));
#201580=CARTESIAN_POINT('Ctrl Pts',(-16.9092612613792,18.1366638317413,
16.1587799007413));
#201581=CARTESIAN_POINT('Ctrl Pts',(-16.9334045226705,18.0966722639571,
16.1614727934465));
#201582=CARTESIAN_POINT('Ctrl Pts',(-16.9612904215477,18.0537576896911,
16.1643677632592));
#201583=CARTESIAN_POINT('Ctrl Pts',(-16.9637399274954,18.0500140868769,
16.1646203466521));
#201584=CARTESIAN_POINT('Ctrl Pts',(-16.9790345291767,18.0268001500309,
16.1661870601097));
#201585=CARTESIAN_POINT('Ctrl Pts',(-16.9921891435605,18.0075349674985,
16.1674892700612));
#201586=CARTESIAN_POINT('Ctrl Pts',(-17.0319377398353,17.9513398163971,
16.171305524648));
#201587=CARTESIAN_POINT('Ctrl Pts',(-17.0594074724403,17.9150448250689,
16.1737937394058));
#201588=CARTESIAN_POINT('Ctrl Pts',(-17.156793091367,17.7946439776979,16.1822247273343));
#201589=CARTESIAN_POINT('Ctrl Pts',(-17.2320430219157,17.7150820989592,
16.1881127371847));
#201590=CARTESIAN_POINT('Ctrl Pts',(-17.3539495572197,17.6047040510136,
16.1972568865666));
#201591=CARTESIAN_POINT('Ctrl Pts',(-17.3962267197886,17.5693277105988,
16.200364295846));
#201592=CARTESIAN_POINT('Ctrl Pts',(-17.4669834401344,17.5146701412555,
16.2055081454606));
#201593=CARTESIAN_POINT('Ctrl Pts',(-17.4946377629391,17.4943617150345,
16.2075052013834));
#201594=CARTESIAN_POINT('Ctrl Pts',(-17.531637095013,17.4685507826268,16.2101657845621));
#201595=CARTESIAN_POINT('Ctrl Pts',(-17.5405490847524,17.4624346632883,
16.2108057849366));
#201596=CARTESIAN_POINT('Ctrl Pts',(-17.5552247269666,17.4525275264622,
16.2118584844579));
#201597=CARTESIAN_POINT('Ctrl Pts',(-17.560960834115,17.4486959121442,16.2122696423624));
#201598=CARTESIAN_POINT('Ctrl Pts',(-17.5721021357031,17.4413322222077,
16.2130677101101));
#201599=CARTESIAN_POINT('Ctrl Pts',(-17.5775049702283,17.4377967021533,
16.2134544845858));
#201600=CARTESIAN_POINT('Ctrl Pts',(-17.5900196113696,17.4296888666572,
16.2143498682619));
#201601=CARTESIAN_POINT('Ctrl Pts',(-17.5971427682634,17.4251343514277,
16.2148591336148));
#201602=CARTESIAN_POINT('Ctrl Pts',(-17.6163783328129,17.4129969361044,
16.2162334632431));
#201603=CARTESIAN_POINT('Ctrl Pts',(-17.6285403913981,17.405493908408,16.2171014557256));
#201604=CARTESIAN_POINT('Ctrl Pts',(-17.7408542435865,17.3377653763361,
16.2251097572964));
#201605=CARTESIAN_POINT('Ctrl Pts',(-17.8457399219199,17.2858161977551,
16.2325519341344));
#201606=CARTESIAN_POINT('Ctrl Pts',(-18.1056902651641,17.1828456766189,
16.2508154733566));
#201607=CARTESIAN_POINT('Ctrl Pts',(-18.2634243809703,17.1405551807621,
16.2617770107206));
#201608=CARTESIAN_POINT('Ctrl Pts',(-18.4565496705893,17.1120089245101,
16.2741813153607));
#201609=CARTESIAN_POINT('Ctrl Pts',(-18.4887611746939,17.1080020432371,
16.2762152702656));
#201610=CARTESIAN_POINT('Ctrl Pts',(-18.5282532198536,17.1040093449202,
16.2786561058693));
#201611=CARTESIAN_POINT('Ctrl Pts',(-18.5354562169685,17.1033183997965,
16.2790991484562));
#201612=CARTESIAN_POINT('Ctrl Pts',(-18.5467547696273,17.1022930250103,
16.2797905907054));
#201613=CARTESIAN_POINT('Ctrl Pts',(-18.5508479181659,17.1019335718734,
16.2800403592994));
#201614=CARTESIAN_POINT('Ctrl Pts',(-18.5585013303763,17.1012839110047,
16.2805059977598));
#201615=CARTESIAN_POINT('Ctrl Pts',(-18.5620612427187,17.1009908002146,
16.2807220227805));
#201616=CARTESIAN_POINT('Ctrl Pts',(-18.5701900166606,17.1003422140641,
16.2812140320091));
#201617=CARTESIAN_POINT('Ctrl Pts',(-18.5747592924736,17.0999925632661,
16.281489686624));
#201618=CARTESIAN_POINT('Ctrl Pts',(-18.5888100791606,17.0989632468895,
16.2823346438884));
#201619=CARTESIAN_POINT('Ctrl Pts',(-18.5982952117365,17.0983325918007,
16.2829012681832));
#201620=CARTESIAN_POINT('Ctrl Pts',(-18.6836872436832,17.0932324468211,
16.2879710614189));
#201621=CARTESIAN_POINT('Ctrl Pts',(-18.759788118296,17.0927912346997,16.2922670377417));
#201622=CARTESIAN_POINT('Ctrl Pts',(-18.8781794958735,17.0984884048164,
16.2988266480516));
#201623=CARTESIAN_POINT('Ctrl Pts',(-18.9205335974498,17.1018062284293,
16.3011483911178));
#201624=CARTESIAN_POINT('Ctrl Pts',(-19.0714390182891,17.11820890987,16.3094125533286));
#201625=CARTESIAN_POINT('Ctrl Pts',(-19.1790385404864,17.138422028434,16.3152991360514));
#201626=CARTESIAN_POINT('Ctrl Pts',(-19.3377692608823,17.1811761884564,
16.3244399676615));
#201627=CARTESIAN_POINT('Ctrl Pts',(-19.3903645225702,17.1975683533973,
16.3275454753109));
#201628=CARTESIAN_POINT('Ctrl Pts',(-19.4745732064122,17.2274637166386,
16.3326864576675));
#201629=CARTESIAN_POINT('Ctrl Pts',(-19.5066030741639,17.2397189051422,
16.3346826055158));
#201630=CARTESIAN_POINT('Ctrl Pts',(-19.5483165266308,17.256852005256,16.3373421503293));
#201631=CARTESIAN_POINT('Ctrl Pts',(-19.5582814039354,17.261034371719,16.337982043846));
#201632=CARTESIAN_POINT('Ctrl Pts',(-19.574553317376,17.2680108853578,16.3390346123738));
#201633=CARTESIAN_POINT('Ctrl Pts',(-19.5808795699397,17.2707599191705,
16.3394457468954));
#201634=CARTESIAN_POINT('Ctrl Pts',(-19.5931016125269,17.2761420950726,
16.3402438012605));
#201635=CARTESIAN_POINT('Ctrl Pts',(-19.5989990192247,17.278771393387,16.3406305859059));
#201636=CARTESIAN_POINT('Ctrl Pts',(-19.612591397065,17.284906114165,16.3415260397565));
#201637=CARTESIAN_POINT('Ctrl Pts',(-19.6202775403846,17.2884307247288,
16.3420353654378));
#201638=CARTESIAN_POINT('Ctrl Pts',(-19.6408989808854,17.298036972484,16.3434099634373));
#201639=CARTESIAN_POINT('Ctrl Pts',(-19.6537939682846,17.3042036431879,
16.3442781657422));
#201640=CARTESIAN_POINT('Ctrl Pts',(-19.7717736487752,17.3620993811035,
16.3523026798732));
#201641=CARTESIAN_POINT('Ctrl Pts',(-19.8724411974683,17.422326909532,16.3597622791222));
#201642=CARTESIAN_POINT('Ctrl Pts',(-20.1005656385797,17.5858979201879,
16.3780997469604));
#201643=CARTESIAN_POINT('Ctrl Pts',(-20.2220273152436,17.6963273176661,
16.389120010295));
#201644=CARTESIAN_POINT('Ctrl Pts',(-20.3502421957089,17.8433595244109,
16.4015038358265));
#201645=CARTESIAN_POINT('Ctrl Pts',(-20.3703945771774,17.8675371837812,
16.4034747427147));
#201646=CARTESIAN_POINT('Ctrl Pts',(-20.3944666239856,17.8977631741408,
16.4058504738676));
#201647=CARTESIAN_POINT('Ctrl Pts',(-20.3989032624609,17.9033924517667,
16.4062892676042));
#201648=CARTESIAN_POINT('Ctrl Pts',(-20.4058289575597,17.9122722781625,
16.4069755603582));
#201649=CARTESIAN_POINT('Ctrl Pts',(-20.408337272522,17.9155076390406,16.4072243955682));
#201650=CARTESIAN_POINT('Ctrl Pts',(-20.4130180100092,17.9215814110329,
16.4076892321713));
#201651=CARTESIAN_POINT('Ctrl Pts',(-20.41519260431,17.9244180154616,16.4079053830788));
#201652=CARTESIAN_POINT('Ctrl Pts',(-20.4201529585156,17.9309224971171,
16.4083989003309));
#201653=CARTESIAN_POINT('Ctrl Pts',(-20.4229339346652,17.9345939603114,
16.4086759292947));
#201654=CARTESIAN_POINT('Ctrl Pts',(-20.4301819902196,17.9442280542002,
16.4093989368037));
#201655=CARTESIAN_POINT('Ctrl Pts',(-20.4346296589565,17.9502053008563,
16.4098435913896));
#201656=CARTESIAN_POINT('Ctrl Pts',(-20.4640845931016,17.9902294087843,
16.412795916421));
#201657=CARTESIAN_POINT('Ctrl Pts',(-20.4881013628316,18.0249972667431,
16.4152399795657));
#201658=CARTESIAN_POINT('Ctrl Pts',(-20.551518383368,18.1229481083979,16.4218682840979));
#201659=CARTESIAN_POINT('Ctrl Pts',(-20.5886525376176,18.1875277514,16.4259559571741));
#201660=CARTESIAN_POINT('Ctrl Pts',(-20.6728512724097,18.353653330175,16.436104231651));
#201661=CARTESIAN_POINT('Ctrl Pts',(-20.7154130829604,18.4572168760118,
16.4421169227898));
#201662=CARTESIAN_POINT('Ctrl Pts',(-20.7754133478612,18.6440361450615,
16.453020106146));
#201663=CARTESIAN_POINT('Ctrl Pts',(-20.7963949659274,18.7258803855298,
16.4578125155934));
#201664=CARTESIAN_POINT('Ctrl Pts',(-20.815132662147,18.8226990448179,16.4636014619307));
#201665=CARTESIAN_POINT('Ctrl Pts',(-20.8176912851591,18.8366720653435,
16.4644396737766));
#201666=CARTESIAN_POINT('Ctrl Pts',(-20.8214097406657,18.8581998135076,
16.4657356903216));
#201667=CARTESIAN_POINT('Ctrl Pts',(-20.8226696393869,18.8657370101307,
16.4661903114204));
#201668=CARTESIAN_POINT('Ctrl Pts',(-20.8248931359332,18.8794965479966,
16.4670218876966));
#201669=CARTESIAN_POINT('Ctrl Pts',(-20.8258698385557,18.8857167053188,
16.4673984219719));
#201670=CARTESIAN_POINT('Ctrl Pts',(-20.8279419771816,18.8993085853143,
16.4682225715453));
#201671=CARTESIAN_POINT('Ctrl Pts',(-20.829026260834,18.9066818999888,16.468670535182));
#201672=CARTESIAN_POINT('Ctrl Pts',(-20.8318905544563,18.9269007283078,
16.4699014048496));
#201673=CARTESIAN_POINT('Ctrl Pts',(-20.8335914777713,18.9397569551365,
16.4706867993473));
#201674=CARTESIAN_POINT('Ctrl Pts',(-20.8416314806901,19.0051410979391,
16.4746956425342));
#201675=CARTESIAN_POINT('Ctrl Pts',(-20.8461174159483,19.0578739552925,
16.4779769208372));
#201676=CARTESIAN_POINT('Ctrl Pts',(-20.8502336389588,19.1446700912249,
16.483460184015));
#201677=CARTESIAN_POINT('Ctrl Pts',(-20.8510257892714,19.1786565838585,
16.4856277414618));
#201678=CARTESIAN_POINT('Ctrl Pts',(-20.8508977921363,19.3432687474514,
16.496218955091));
#201679=CARTESIAN_POINT('Ctrl Pts',(-20.8387067175164,19.4735944789054,
16.5049104950054));
#201680=CARTESIAN_POINT('Ctrl Pts',(-20.7970384800906,19.695346905119,16.5197604038486));
#201681=CARTESIAN_POINT('Ctrl Pts',(-20.7732180830191,19.787466454308,16.5259401923999));
#201682=CARTESIAN_POINT('Ctrl Pts',(-20.7402342477503,19.8868749495494,
16.5324112593424));
#201683=CARTESIAN_POINT('Ctrl Pts',(-20.7371210656065,19.896046574314,16.5330063461856));
#201684=CARTESIAN_POINT('Ctrl Pts',(-20.7324307951557,19.9095590020489,
16.5338798603169));
#201685=CARTESIAN_POINT('Ctrl Pts',(-20.7309023232884,19.9139163780622,
16.5341610472707));
#201686=CARTESIAN_POINT('Ctrl Pts',(-20.728165063313,19.9216387860185,16.5346584573051));
#201687=CARTESIAN_POINT('Ctrl Pts',(-20.726961996427,19.9250057880776,16.5348750146441));
#201688=CARTESIAN_POINT('Ctrl Pts',(-20.7247001936944,19.9312855986208,
16.5352783186923));
#201689=CARTESIAN_POINT('Ctrl Pts',(-20.7236436008293,19.9341991058504,
16.5354651930116));
#201690=CARTESIAN_POINT('Ctrl Pts',(-20.7225806064499,19.9371103026755,
16.5356516909487));
#201691=CARTESIAN_POINT('Origin',(-18.734,19.211,0.));
#201692=CARTESIAN_POINT('',(-20.722580618353,19.9371102700768,17.5536949396865));
#201693=CARTESIAN_POINT('',(-20.7225806054526,19.9371103054067,17.3329786569753));
#201694=CARTESIAN_POINT('',(-20.7225806064498,19.9371103026755,0.));
#201695=CARTESIAN_POINT('',(-20.8509990201954,19.2127872399449,17.5117108857594));
#201696=CARTESIAN_POINT('Ctrl Pts',(-20.722580618353,19.9371102700768,17.5536949396865));
#201697=CARTESIAN_POINT('Ctrl Pts',(-20.7266413316867,19.9259892927749,
17.5529480158583));
#201698=CARTESIAN_POINT('Ctrl Pts',(-20.7306095645022,19.9148320356873,
17.5522050109842));
#201699=CARTESIAN_POINT('Ctrl Pts',(-20.7395308685426,19.8890654862418,
17.5505046497996));
#201700=CARTESIAN_POINT('Ctrl Pts',(-20.7444177097079,19.8744361555218,
17.549550649084));
#201701=CARTESIAN_POINT('Ctrl Pts',(-20.7509063836573,19.8542811970314,
17.5482531686163));
#201702=CARTESIAN_POINT('Ctrl Pts',(-20.7526460934486,19.8488009172698,
17.5479020745191));
#201703=CARTESIAN_POINT('Ctrl Pts',(-20.7553799364389,19.8400657627298,
17.5473452367977));
#201704=CARTESIAN_POINT('Ctrl Pts',(-20.7563885709251,19.8368155078355,
17.5471386545693));
#201705=CARTESIAN_POINT('Ctrl Pts',(-20.758459556094,19.8300846056304,17.5467121308139));
#201706=CARTESIAN_POINT('Ctrl Pts',(-20.7595207706185,19.8266036477637,
17.5464922617105));
#201707=CARTESIAN_POINT('Ctrl Pts',(-20.7620345457301,19.8182811796242,
17.5459682526278));
#201708=CARTESIAN_POINT('Ctrl Pts',(-20.7634787639705,19.8134371316568,
17.5456645993725));
#201709=CARTESIAN_POINT('Ctrl Pts',(-20.7683204546765,19.7969826202226,
17.5446375424508));
#201710=CARTESIAN_POINT('Ctrl Pts',(-20.7716358259506,19.7853479778766,
17.5439187643947));
#201711=CARTESIAN_POINT('Ctrl Pts',(-20.7896326232094,19.7200738513861,
17.5399243904783));
#201712=CARTESIAN_POINT('Ctrl Pts',(-20.8022969819697,19.6658959757595,
17.536752744696));
#201713=CARTESIAN_POINT('Ctrl Pts',(-20.8381002120249,19.4799544656379,
17.5261607586984));
#201714=CARTESIAN_POINT('Ctrl Pts',(-20.8508862152965,19.3465296112034,
17.519037359307));
#201715=CARTESIAN_POINT('Ctrl Pts',(-20.8509992439645,19.2127891489275,
17.5117113811062));
#201716=CARTESIAN_POINT('Ctrl Pts',(-20.8509992455948,19.212787218789,17.5117112753779));
#201717=CARTESIAN_POINT('Ctrl Pts',(-20.8510695258044,19.1295387930481,
17.5071511275068));
#201718=CARTESIAN_POINT('Ctrl Pts',(-20.8462293912133,19.0463633492458,
17.5025270677366));
#201719=CARTESIAN_POINT('Ctrl Pts',(-20.8325134454039,18.9297566661536,
17.4958024627517));
#201720=CARTESIAN_POINT('Ctrl Pts',(-20.8277010588129,18.895925120176,17.4938229102094));
#201721=CARTESIAN_POINT('Ctrl Pts',(-20.8203844052654,18.8521210862257,
17.4912165343719));
#201722=CARTESIAN_POINT('Ctrl Pts',(-20.8186232314416,18.8420285394258,
17.4906130217416));
#201723=CARTESIAN_POINT('Ctrl Pts',(-20.8155220286154,18.8249882045327,
17.489588800915));
#201724=CARTESIAN_POINT('Ctrl Pts',(-20.8142202866628,18.8180335650957,
17.4891693060336));
#201725=CARTESIAN_POINT('Ctrl Pts',(-20.8115755295169,18.8042852649797,
17.4883370327338));
#201726=CARTESIAN_POINT('Ctrl Pts',(-20.8102339941972,18.7974914074432,
17.4879243060368));
#201727=CARTESIAN_POINT('Ctrl Pts',(-20.8075793288925,18.7843862130888,
17.4871253128691));
#201728=CARTESIAN_POINT('Ctrl Pts',(-20.806270655976,18.7780740440354,17.4867391930152));
#201729=CARTESIAN_POINT('Ctrl Pts',(-20.8031923941714,18.7635603597318,
17.4858483855784));
#201730=CARTESIAN_POINT('Ctrl Pts',(-20.8014028458251,18.7553632305344,
17.4853430629542));
#201731=CARTESIAN_POINT('Ctrl Pts',(-20.7964824081128,18.7334508131591,
17.4839862327915));
#201732=CARTESIAN_POINT('Ctrl Pts',(-20.7932634947401,18.7197559121355,
17.483131911935));
#201733=CARTESIAN_POINT('Ctrl Pts',(-20.7650016192786,18.6046773257395,
17.4758985085358));
#201734=CARTESIAN_POINT('Ctrl Pts',(-20.7326286782233,18.5052574780061,
17.4692808211591));
#201735=CARTESIAN_POINT('Ctrl Pts',(-20.6611667090069,18.3307737651146,
17.4570259400451));
#201736=CARTESIAN_POINT('Ctrl Pts',(-20.6246612391262,18.2548783344609,
17.4514610948834));
#201737=CARTESIAN_POINT('Ctrl Pts',(-20.5387681077716,18.100572081465,17.4397939993481));
#201738=CARTESIAN_POINT('Ctrl Pts',(-20.4885501277334,18.0228104374067,
17.4337049592147));
#201739=CARTESIAN_POINT('Ctrl Pts',(-20.4146638440853,17.9233487510274,
17.4258399888688));
#201740=CARTESIAN_POINT('Ctrl Pts',(-20.3953620683474,17.8985393271178,
17.4238717384569));
#201741=CARTESIAN_POINT('Ctrl Pts',(-20.3709897443403,17.8686122375115,
17.4214987552279));
#201742=CARTESIAN_POINT('Ctrl Pts',(-20.3664373888904,17.8630799346069,
17.4210601439086));
#201743=CARTESIAN_POINT('Ctrl Pts',(-20.3592401808988,17.8544233866523,
17.4203740723007));
#201744=CARTESIAN_POINT('Ctrl Pts',(-20.3566142520256,17.851283579834,17.4201252772176));
#201745=CARTESIAN_POINT('Ctrl Pts',(-20.3516781455532,17.84541617114,17.4196604748008));
#201746=CARTESIAN_POINT('Ctrl Pts',(-20.3493701927867,17.8426868352907,
17.419444318196));
#201747=CARTESIAN_POINT('Ctrl Pts',(-20.3440718016724,17.8364531598767,
17.4189507348051));
#201748=CARTESIAN_POINT('Ctrl Pts',(-20.3410768354129,17.8329527336724,
17.41867364574));
#201749=CARTESIAN_POINT('Ctrl Pts',(-20.3332062439371,17.8238143793443,
17.4179503781609));
#201750=CARTESIAN_POINT('Ctrl Pts',(-20.328312179245,17.8181923192279,17.4175055251567));
#201751=CARTESIAN_POINT('Ctrl Pts',(-20.2954412706125,17.7808321234847,
17.4145491856431));
#201752=CARTESIAN_POINT('Ctrl Pts',(-20.2665460195083,17.7499105996997,
17.4121015032233));
#201753=CARTESIAN_POINT('Ctrl Pts',(-20.1846540736877,17.6673807644727,
17.4054976604523));
#201754=CARTESIAN_POINT('Ctrl Pts',(-20.1298485030154,17.6176494414284,
17.4014360247064));
#201755=CARTESIAN_POINT('Ctrl Pts',(-20.0033179293491,17.5143838268614,
17.3925359590513));
#201756=CARTESIAN_POINT('Ctrl Pts',(-19.9305795752396,17.4623229092268,
17.3877189274544));
#201757=CARTESIAN_POINT('Ctrl Pts',(-19.7945061473346,17.3774074393543,
17.3788987899348));
#201758=CARTESIAN_POINT('Ctrl Pts',(-19.7323923789462,17.3428601679122,
17.374937965075));
#201759=CARTESIAN_POINT('Ctrl Pts',(-19.6443228075205,17.2995248416322,
17.3693227495859));
#201760=CARTESIAN_POINT('Ctrl Pts',(-19.6197553696905,17.2880173618407,
17.3677567025062));
#201761=CARTESIAN_POINT('Ctrl Pts',(-19.5768209842197,17.2689040594172,
17.3650161569712));
#201762=CARTESIAN_POINT('Ctrl Pts',(-19.5585552173372,17.2610788457664,
17.3638491100963));
#201763=CARTESIAN_POINT('Ctrl Pts',(-19.5321199541511,17.2501916033565,
17.3621573736208));
#201764=CARTESIAN_POINT('Ctrl Pts',(-19.5240371149384,17.2469209834848,
17.3616397490928));
#201765=CARTESIAN_POINT('Ctrl Pts',(-19.5098882815928,17.2412973054451,
17.3607329365963));
#201766=CARTESIAN_POINT('Ctrl Pts',(-19.5038311777474,17.2389220890745,
17.3603445013724));
#201767=CARTESIAN_POINT('Ctrl Pts',(-19.4921774263775,17.234414089723,17.3595966801764));
#201768=CARTESIAN_POINT('Ctrl Pts',(-19.4865824809732,17.2322770586158,
17.3592374414597));
#201769=CARTESIAN_POINT('Ctrl Pts',(-19.4719319566534,17.2267523069803,
17.3582961759277));
#201770=CARTESIAN_POINT('Ctrl Pts',(-19.4628621817998,17.223402858979,17.357712875464));
#201771=CARTESIAN_POINT('Ctrl Pts',(-19.4314552563128,17.2120482265024,
17.3556908127909));
#201772=CARTESIAN_POINT('Ctrl Pts',(-19.4090073084605,17.2043567609148,
17.3542416968103));
#201773=CARTESIAN_POINT('Ctrl Pts',(-19.2315960822488,17.1468831061675,
17.3427547134132));
#201774=CARTESIAN_POINT('Ctrl Pts',(-19.07151605238,17.1147546816393,17.3321225323069));
#201775=CARTESIAN_POINT('Ctrl Pts',(-18.7800578764075,17.0905271206785,
17.3127961273034));
#201776=CARTESIAN_POINT('Ctrl Pts',(-18.6500163194528,17.0916887461439,
17.3042053638423));
#201777=CARTESIAN_POINT('Ctrl Pts',(-18.5090085419455,17.1059559518949,
17.2954160528913));
#201778=CARTESIAN_POINT('Ctrl Pts',(-18.4971377171314,17.1072586008024,
17.2946803677359));
#201779=CARTESIAN_POINT('Ctrl Pts',(-18.4802847913946,17.1092524232285,
17.2936425705466));
#201780=CARTESIAN_POINT('Ctrl Pts',(-18.4752934025745,17.1098609800424,
17.2933360330874));
#201781=CARTESIAN_POINT('Ctrl Pts',(-18.4666980282372,17.1109400329748,
17.2928096501668));
#201782=CARTESIAN_POINT('Ctrl Pts',(-18.4630930146798,17.1114020348425,
17.2925893299845));
#201783=CARTESIAN_POINT('Ctrl Pts',(-18.4561076967961,17.1123155316816,
17.2921633184898));
#201784=CARTESIAN_POINT('Ctrl Pts',(-18.4527272938496,17.1127659103674,
17.291957563008));
#201785=CARTESIAN_POINT('Ctrl Pts',(-18.4436144981057,17.1140024467796,
17.2914039477744));
#201786=CARTESIAN_POINT('Ctrl Pts',(-18.4378841668616,17.1148039468894,
17.2910569481935));
#201787=CARTESIAN_POINT('Ctrl Pts',(-18.4166551314657,17.1178620368697,
17.289775364405));
#201788=CARTESIAN_POINT('Ctrl Pts',(-18.4011778915775,17.1202671680025,
17.2888488011517));
#201789=CARTESIAN_POINT('Ctrl Pts',(-18.252272384081,17.1451022749719,17.2799972890781));
#201790=CARTESIAN_POINT('Ctrl Pts',(-18.1212383384864,17.1801065615635,
17.2726831911094));
#201791=CARTESIAN_POINT('Ctrl Pts',(-17.8484332178777,17.2818193034361,
17.2568724230478));
#201792=CARTESIAN_POINT('Ctrl Pts',(-17.7089125452259,17.3521953041116,
17.2483887314886));
#201793=CARTESIAN_POINT('Ctrl Pts',(-17.5605579158077,17.4488492587841,
17.2380771526044));
#201794=CARTESIAN_POINT('Ctrl Pts',(-17.542910159438,17.4607295915006,17.2368287834525));
#201795=CARTESIAN_POINT('Ctrl Pts',(-17.5180639563392,17.4780056680327,
17.2350386133694));
#201796=CARTESIAN_POINT('Ctrl Pts',(-17.5107158709621,17.4831846878929,
17.2345050512705));
#201797=CARTESIAN_POINT('Ctrl Pts',(-17.4980935244035,17.4922019518258,
17.2335812464766));
#201798=CARTESIAN_POINT('Ctrl Pts',(-17.4928035672132,17.4960180873847,
17.2331918580774));
#201799=CARTESIAN_POINT('Ctrl Pts',(-17.4827067162483,17.5033730656228,
17.2324443210061));
#201800=CARTESIAN_POINT('Ctrl Pts',(-17.4778969808966,17.5069079152705,
17.2320863297524));
#201801=CARTESIAN_POINT('Ctrl Pts',(-17.4654245909403,17.5161558223313,
17.2311530223009));
#201802=CARTESIAN_POINT('Ctrl Pts',(-17.4577856266262,17.5219004696122,
17.2305764741588));
#201803=CARTESIAN_POINT('Ctrl Pts',(-17.4318476333021,17.541682738521,17.2286017440046));
#201804=CARTESIAN_POINT('Ctrl Pts',(-17.4137397196967,17.5559671810501,
17.2271938462437));
#201805=CARTESIAN_POINT('Ctrl Pts',(-17.2606301533132,17.6808596672632,
17.2150311543126));
#201806=CARTESIAN_POINT('Ctrl Pts',(-17.139575770845,17.807455753402,17.2035813786229));
#201807=CARTESIAN_POINT('Ctrl Pts',(-16.9831079609131,18.0177877742928,
17.1862602023824));
#201808=CARTESIAN_POINT('Ctrl Pts',(-16.9351878379651,18.0913325993497,
17.1804793097828));
#201809=CARTESIAN_POINT('Ctrl Pts',(-16.8732399865028,18.2007006882016,
17.1724531482782));
#201810=CARTESIAN_POINT('Ctrl Pts',(-16.8554068138177,18.2342602274371,
17.1700629668203));
#201811=CARTESIAN_POINT('Ctrl Pts',(-16.8351093785287,18.2750721788775,
17.1672580674368));
#201812=CARTESIAN_POINT('Ctrl Pts',(-16.8317697243615,18.2818786617992,
17.166793611509));
#201813=CARTESIAN_POINT('Ctrl Pts',(-16.8266436821056,18.2924694422797,
17.1660762598677));
#201814=CARTESIAN_POINT('Ctrl Pts',(-16.8248318664517,18.296241262725,17.1658218251893));
#201815=CARTESIAN_POINT('Ctrl Pts',(-16.8214977704639,18.3032352061702,
17.1653520020817));
#201816=CARTESIAN_POINT('Ctrl Pts',(-16.8199724555475,18.3064557731787,
17.165136430739));
#201817=CARTESIAN_POINT('Ctrl Pts',(-16.816549056206,18.3137314094614,17.1646511591042));
#201818=CARTESIAN_POINT('Ctrl Pts',(-16.814655704842,18.317788646,17.164381752898));
#201819=CARTESIAN_POINT('Ctrl Pts',(-16.8091243790593,18.3297404459087,
17.1635915853232));
#201820=CARTESIAN_POINT('Ctrl Pts',(-16.8055220882627,18.3376515543186,
17.1630729720515));
#201821=CARTESIAN_POINT('Ctrl Pts',(-16.7804016249692,18.3937327552829,
17.1594261287749));
#201822=CARTESIAN_POINT('Ctrl Pts',(-16.7606401043972,18.4426745011667,
17.1563970382605));
#201823=CARTESIAN_POINT('Ctrl Pts',(-16.7373109645124,18.5073123117826,
17.1525305064271));
#201824=CARTESIAN_POINT('Ctrl Pts',(-16.7320651426583,18.5223779613646,
17.1516385895809));
#201825=CARTESIAN_POINT('Ctrl Pts',(-16.7108725009644,18.585531565523,17.147933023092));
#201826=CARTESIAN_POINT('Ctrl Pts',(-16.6964837281179,18.6341261617481,
17.1451614273198));
#201827=CARTESIAN_POINT('Ctrl Pts',(-16.6565747464857,18.7891432622963,
17.1364461509989));
#201828=CARTESIAN_POINT('Ctrl Pts',(-16.6375523632505,18.8970490160094,
17.1305552825568));
#201829=CARTESIAN_POINT('Ctrl Pts',(-16.6216102414295,19.0608561422268,
17.1214044868495));
#201830=CARTESIAN_POINT('Ctrl Pts',(-16.6184148836214,19.1159598080599,
17.1182932675612));
#201831=CARTESIAN_POINT('Ctrl Pts',(-16.61672878575,19.205455191344,17.1131436738121));
#201832=CARTESIAN_POINT('Ctrl Pts',(-16.6169174114437,19.2397968004508,
17.1111447992172));
#201833=CARTESIAN_POINT('Ctrl Pts',(-16.6182634819072,19.2849249316174,
17.1084821365268));
#201834=CARTESIAN_POINT('Ctrl Pts',(-16.6186686401239,19.2957298109645,
17.1078419222804));
#201835=CARTESIAN_POINT('Ctrl Pts',(-16.6194678656833,19.3134228906346,
17.1067889605801));
#201836=CARTESIAN_POINT('Ctrl Pts',(-16.6198128701462,19.3203131913915,
17.1063777558761));
#201837=CARTESIAN_POINT('Ctrl Pts',(-16.6205459420015,19.3336484054593,
17.1055796613158));
#201838=CARTESIAN_POINT('Ctrl Pts',(-16.6209298263292,19.3400934790852,
17.105192907166));
#201839=CARTESIAN_POINT('Ctrl Pts',(-16.6218843586192,19.3549721062545,
17.104297663796));
#201840=CARTESIAN_POINT('Ctrl Pts',(-16.6224760433415,19.3634041573075,
17.1037885190704));
#201841=CARTESIAN_POINT('Ctrl Pts',(-16.6242033358871,19.3860744131268,
17.1024147259844));
#201842=CARTESIAN_POINT('Ctrl Pts',(-16.6254325547246,19.4003048521906,
17.1015471529727));
#201843=CARTESIAN_POINT('Ctrl Pts',(-16.6403646641977,19.5549069822277,
17.0920633076009));
#201844=CARTESIAN_POINT('Ctrl Pts',(-16.6679158734398,19.6935598094669,
17.0829974680668));
#201845=CARTESIAN_POINT('Ctrl Pts',(-16.7372099462143,19.9208242679886,
17.0673666161625));
#201846=CARTESIAN_POINT('Ctrl Pts',(-16.7716755157006,20.0111898685889,
17.0609407118479));
#201847=CARTESIAN_POINT('Ctrl Pts',(-16.832738690007,20.143359639222,17.0514397387777));
#201848=CARTESIAN_POINT('Ctrl Pts',(-16.8548246766492,20.1871095245703,
17.048278174716));
#201849=CARTESIAN_POINT('Ctrl Pts',(-16.8910509596667,20.2530736162929,
17.0435258520863));
#201850=CARTESIAN_POINT('Ctrl Pts',(-16.9041195477913,20.2758550438793,
17.0418874260181));
#201851=CARTESIAN_POINT('Ctrl Pts',(-16.921081490268,20.3041885347935,17.0398589111108));
#201852=CARTESIAN_POINT('Ctrl Pts',(-16.9245814732206,20.3099719256345,
17.039445345445));
#201853=CARTESIAN_POINT('Ctrl Pts',(-16.930198322323,20.3191536604977,17.0387896766877));
#201854=CARTESIAN_POINT('Ctrl Pts',(-16.9322971956717,20.3225628786332,
17.0385464250224));
#201855=CARTESIAN_POINT('Ctrl Pts',(-16.9362980700381,20.32902042937,17.0380860843603));
#201856=CARTESIAN_POINT('Ctrl Pts',(-16.9381981361603,20.3320698352292,
17.0378688803502));
#201857=CARTESIAN_POINT('Ctrl Pts',(-16.9425919068582,20.3390815402062,
17.037369838551));
#201858=CARTESIAN_POINT('Ctrl Pts',(-16.9450909970951,20.3430404135086,
17.0370883604774));
#201859=CARTESIAN_POINT('Ctrl Pts',(-16.951828846634,20.3536359838918,17.0363356854586));
#201860=CARTESIAN_POINT('Ctrl Pts',(-16.9560915842328,20.3602574476933,
17.0358660325559));
#201861=CARTESIAN_POINT('Ctrl Pts',(-16.9884189013182,20.4098622928407,
17.0323517870805));
#201862=CARTESIAN_POINT('Ctrl Pts',(-17.0180040786294,20.4518396696527,
17.0294014473958));
#201863=CARTESIAN_POINT('Ctrl Pts',(-17.0626484294944,20.5105285820624,
17.0252474284108));
#201864=CARTESIAN_POINT('Ctrl Pts',(-17.0764904465676,20.5281380858821,
17.0239970768856));
#201865=CARTESIAN_POINT('Ctrl Pts',(-17.1195404441598,20.5811516675939,
17.0202098749172));
#201866=CARTESIAN_POINT('Ctrl Pts',(-17.1496229850703,20.6158291585129,
17.0177003067727));
#201867=CARTESIAN_POINT('Ctrl Pts',(-17.2551144918941,20.7297312272389,
17.0092479120587));
#201868=CARTESIAN_POINT('Ctrl Pts',(-17.3355231997998,20.8040814927553,
17.0033597070467));
#201869=CARTESIAN_POINT('Ctrl Pts',(-17.4645504801973,20.906058803431,16.9942151039222));
#201870=CARTESIAN_POINT('Ctrl Pts',(-17.5091044536831,20.9385290693859,
16.9911074345531));
#201871=CARTESIAN_POINT('Ctrl Pts',(-17.583366686089,20.9883320114188,16.9859631927978));
#201872=CARTESIAN_POINT('Ctrl Pts',(-17.6123201583285,21.0067450370439,
16.9839660126999));
#201873=CARTESIAN_POINT('Ctrl Pts',(-17.6509662659385,21.0300227504618,
16.981305287538));
#201874=CARTESIAN_POINT('Ctrl Pts',(-17.6602678723747,21.0355287466519,
16.980665272561));
#201875=CARTESIAN_POINT('Ctrl Pts',(-17.6755740106148,21.0444314850177,
16.979612555143));
#201876=CARTESIAN_POINT('Ctrl Pts',(-17.6815537746091,21.047870579597,16.9792013940473));
#201877=CARTESIAN_POINT('Ctrl Pts',(-17.6931630156139,21.0544720129312,
16.9784033244816));
#201878=CARTESIAN_POINT('Ctrl Pts',(-17.6987903681982,21.0576379470049,
16.978016551402));
#201879=CARTESIAN_POINT('Ctrl Pts',(-17.711819513031,21.0648898384521,16.9771211773324));
#201880=CARTESIAN_POINT('Ctrl Pts',(-17.7192314379364,21.0689572770288,
16.9766119202343));
#201881=CARTESIAN_POINT('Ctrl Pts',(-17.7392357645613,21.0797796315547,
16.975237627312));
#201882=CARTESIAN_POINT('Ctrl Pts',(-17.7518723558361,21.0864515377035,
16.9743696635239));
#201883=CARTESIAN_POINT('Ctrl Pts',(-17.868436067835,21.1464940726931,16.9663635436742));
#201884=CARTESIAN_POINT('Ctrl Pts',(-17.9765299840583,21.191295330932,16.9589237105708));
#201885=CARTESIAN_POINT('Ctrl Pts',(-18.2426496289494,21.2766047339658,
16.9406697243583));
#201886=CARTESIAN_POINT('Ctrl Pts',(-18.4027502413841,21.3082414656108,
16.9297156680553));
#201887=CARTESIAN_POINT('Ctrl Pts',(-18.5973698628822,21.3238375975069,
16.9173086143513));
#201888=CARTESIAN_POINT('Ctrl Pts',(-18.6299044169844,21.3256902580934,
16.9152664910865));
#201889=CARTESIAN_POINT('Ctrl Pts',(-18.6697112111448,21.3270360195069,
16.9128172364443));
#201890=CARTESIAN_POINT('Ctrl Pts',(-18.6769530041953,21.3272436362545,
16.9123736544594));
#201891=CARTESIAN_POINT('Ctrl Pts',(-18.6883054688174,21.3275107862288,
16.9116815586666));
#201892=CARTESIAN_POINT('Ctrl Pts',(-18.6924154112572,21.3275955260858,
16.9114316717471));
#201893=CARTESIAN_POINT('Ctrl Pts',(-18.7000967838712,21.3277315203358,
16.9109659307326));
#201894=CARTESIAN_POINT('Ctrl Pts',(-18.703668057698,21.3277857073295,16.9107499207706));
#201895=CARTESIAN_POINT('Ctrl Pts',(-18.7118188566586,21.3278887477691,
16.9102580985994));
#201896=CARTESIAN_POINT('Ctrl Pts',(-18.7163984049109,21.3279317793226,
16.9099826150137));
#201897=CARTESIAN_POINT('Ctrl Pts',(-18.7304690043151,21.3280183307256,
16.9091387027651));
#201898=CARTESIAN_POINT('Ctrl Pts',(-18.739960387906,21.3280128865746,16.9085729428504));
#201899=CARTESIAN_POINT('Ctrl Pts',(-18.8248973036766,21.3273929303706,
16.903538866284));
#201900=CARTESIAN_POINT('Ctrl Pts',(-18.9002684909403,21.3228093449835,
16.8992745218673));
#201901=CARTESIAN_POINT('Ctrl Pts',(-19.0180313935093,21.3093017471572,
16.8927122355578));
#201902=CARTESIAN_POINT('Ctrl Pts',(-19.0606625734108,21.3030888626568,
16.89035771035));
#201903=CARTESIAN_POINT('Ctrl Pts',(-19.2107257497164,21.2765201275709,
16.8820607041474));
#201904=CARTESIAN_POINT('Ctrl Pts',(-19.3167367988922,21.2491505769794,
16.8761738528689));
#201905=CARTESIAN_POINT('Ctrl Pts',(-19.4722619360478,21.1958657558821,
16.8670323969262));
#201906=CARTESIAN_POINT('Ctrl Pts',(-19.5236483769392,21.1759879265342,
16.8639265314401));
#201907=CARTESIAN_POINT('Ctrl Pts',(-19.6056761109337,21.1405195838339,
16.8587850095325));
#201908=CARTESIAN_POINT('Ctrl Pts',(-19.636816585931,21.1261467522292,16.8567886907969));
#201909=CARTESIAN_POINT('Ctrl Pts',(-19.6772926677318,21.1062584893208,
16.8541289505809));
#201910=CARTESIAN_POINT('Ctrl Pts',(-19.6869555537995,21.1014183410733,
16.8534890369579));
#201911=CARTESIAN_POINT('Ctrl Pts',(-19.7027243664439,21.0933681047734,
16.8524364437869));
#201912=CARTESIAN_POINT('Ctrl Pts',(-19.7088524881154,21.0902017466717,
16.8520253048699));
#201913=CARTESIAN_POINT('Ctrl Pts',(-19.7206868970349,21.0840135236379,
16.8512272479995));
#201914=CARTESIAN_POINT('Ctrl Pts',(-19.7263950550936,21.0809953865461,
16.8508404652758));
#201915=CARTESIAN_POINT('Ctrl Pts',(-19.7395461228862,21.0739647048852,
16.8499450246546));
#201916=CARTESIAN_POINT('Ctrl Pts',(-19.7469789411445,21.0699336078668,
16.8494357103421));
#201917=CARTESIAN_POINT('Ctrl Pts',(-19.7669104048741,21.0589689887334,
16.848061162904));
#201918=CARTESIAN_POINT('Ctrl Pts',(-19.7793631444333,21.0519533313886,
16.847193000127));
#201919=CARTESIAN_POINT('Ctrl Pts',(-19.8931592602747,20.9863156852671,
16.8391715748319));
#201920=CARTESIAN_POINT('Ctrl Pts',(-19.9895309153828,20.9195169718493,
16.8317152957038));
#201921=CARTESIAN_POINT('Ctrl Pts',(-20.2060400843744,20.7411966124897,
16.8133923465813));
#201922=CARTESIAN_POINT('Ctrl Pts',(-20.3197428723568,20.6230281197913,
16.802383734368));
#201923=CARTESIAN_POINT('Ctrl Pts',(-20.4378917579976,20.4677594710626,
16.7899959996778));
#201924=CARTESIAN_POINT('Ctrl Pts',(-20.4564984102092,20.4421340167836,
16.78801273413));
#201925=CARTESIAN_POINT('Ctrl Pts',(-20.4786120200789,20.4101953407588,
16.7856242240604));
#201926=CARTESIAN_POINT('Ctrl Pts',(-20.4826697620295,20.404270561386,16.7851845853515));
#201927=CARTESIAN_POINT('Ctrl Pts',(-20.4889950222431,20.3949333829763,
16.7844972683068));
#201928=CARTESIAN_POINT('Ctrl Pts',(-20.4912828720863,20.3915349175494,
16.7842482472938));
#201929=CARTESIAN_POINT('Ctrl Pts',(-20.4955480358932,20.3851593969218,
16.7837832521015));
#201930=CARTESIAN_POINT('Ctrl Pts',(-20.4975276542473,20.3821840099075,
16.7835671272824));
#201931=CARTESIAN_POINT('Ctrl Pts',(-20.5020387383687,20.3753664326526,
16.7830739149219));
#201932=CARTESIAN_POINT('Ctrl Pts',(-20.5045652144511,20.3715210003067,
16.7827971631906));
#201933=CARTESIAN_POINT('Ctrl Pts',(-20.5111412917283,20.3614403959901,
16.7820753549154));
#201934=CARTESIAN_POINT('Ctrl Pts',(-20.5151706592888,20.3551920125831,
16.7816316151908));
#201935=CARTESIAN_POINT('Ctrl Pts',(-20.5417145229974,20.3135501301173,
16.7786977146286));
#201936=CARTESIAN_POINT('Ctrl Pts',(-20.5632073643183,20.2775127907092,
16.7762702620137));
#201937=CARTESIAN_POINT('Ctrl Pts',(-20.5941806202874,20.2218850718296,
16.7726525679296));
#201938=CARTESIAN_POINT('Ctrl Pts',(-20.6044523717743,20.2027502432319,
16.7714306122185));
#201939=CARTESIAN_POINT('Ctrl Pts',(-20.6222715811604,20.1682935721515,
16.7692641207855));
#201940=CARTESIAN_POINT('Ctrl Pts',(-20.6299313569032,20.1530323012153,
16.7683162021039));
#201941=CARTESIAN_POINT('Ctrl Pts',(-20.6692389896475,20.0722941905844,
16.7633540472585));
#201942=CARTESIAN_POINT('Ctrl Pts',(-20.6976644695323,20.0053475411258,
16.7594186685798));
#201943=CARTESIAN_POINT('Ctrl Pts',(-20.7225806782305,19.9371101060915,
16.7554729098499));
#201944=CARTESIAN_POINT('',(-20.8509999221906,19.2115739728967,17.290908287241));
#201945=CARTESIAN_POINT('Ctrl Pts',(-20.7225806064499,19.9371103026755,
16.5356516909487));
#201946=CARTESIAN_POINT('Ctrl Pts',(-20.7222420517169,19.9380374942795,
16.5357110889667));
#201947=CARTESIAN_POINT('Ctrl Pts',(-20.7219028476344,19.9389644515232,
16.5357704488057));
#201948=CARTESIAN_POINT('Ctrl Pts',(-20.7191070447656,19.9465881332496,
16.5362584608096));
#201949=CARTESIAN_POINT('Ctrl Pts',(-20.7166172235478,19.9532727457913,
16.5366851668454));
#201950=CARTESIAN_POINT('Ctrl Pts',(-20.7031297565641,19.9889315139748,
16.5389556645996));
#201951=CARTESIAN_POINT('Ctrl Pts',(-20.6915300434208,20.0176757689274,
16.5407655708978));
#201952=CARTESIAN_POINT('Ctrl Pts',(-20.6147735820571,20.196462055387,16.5519561572183));
#201953=CARTESIAN_POINT('Ctrl Pts',(-20.5330352019228,20.3387984850848,
16.5606012946165));
#201954=CARTESIAN_POINT('Ctrl Pts',(-20.365712353063,20.5649020204647,16.5759958048462));
#201955=CARTESIAN_POINT('Ctrl Pts',(-20.2879589469206,20.6534777757539,
16.5825622185153));
#201956=CARTESIAN_POINT('Ctrl Pts',(-20.1929613282677,20.7450551973625,
16.5902922217907));
#201957=CARTESIAN_POINT('Ctrl Pts',(-20.1825655610694,20.754875417991,16.5911343486701));
#201958=CARTESIAN_POINT('Ctrl Pts',(-20.1658644156388,20.7703347394152,
16.5924817339191));
#201959=CARTESIAN_POINT('Ctrl Pts',(-20.1596232413558,20.7760427805206,
16.5929840455174));
#201960=CARTESIAN_POINT('Ctrl Pts',(-20.1485570613111,20.7860425446627,
16.5938726688127));
#201961=CARTESIAN_POINT('Ctrl Pts',(-20.1437462830484,20.7903499020825,
16.5942583134681));
#201962=CARTESIAN_POINT('Ctrl Pts',(-20.1337566230684,20.7992121910514,
16.5950577828901));
#201963=CARTESIAN_POINT('Ctrl Pts',(-20.1285750439512,20.8037639538443,
16.5954717334905));
#201964=CARTESIAN_POINT('Ctrl Pts',(-20.1152202468021,20.8153803600855,
16.5965368249411));
#201965=CARTESIAN_POINT('Ctrl Pts',(-20.1070151002742,20.8224078433618,
16.5971894929732));
#201966=CARTESIAN_POINT('Ctrl Pts',(-20.0725673194657,20.8514573043545,
16.5999227642694));
#201967=CARTESIAN_POINT('Ctrl Pts',(-20.0458470612861,20.8729024365244,
16.6020266394149));
#201968=CARTESIAN_POINT('Ctrl Pts',(-19.9749015891035,20.9270645174338,
16.6075744238814));
#201969=CARTESIAN_POINT('Ctrl Pts',(-19.9299029338047,20.9587212415474,
16.611056603408));
#201970=CARTESIAN_POINT('Ctrl Pts',(-19.8068132698785,21.038334370842,16.6204783693331));
#201971=CARTESIAN_POINT('Ctrl Pts',(-19.7267584986212,21.0830329964801,
16.6265051250854));
#201972=CARTESIAN_POINT('Ctrl Pts',(-19.5956079726278,21.1454770180192,
16.6361029179627));
#201973=CARTESIAN_POINT('Ctrl Pts',(-19.5462882637157,21.1666987433982,
16.6396529510337));
#201974=CARTESIAN_POINT('Ctrl Pts',(-19.4618372415616,21.1992906688597,
16.6455883741705));
#201975=CARTESIAN_POINT('Ctrl Pts',(-19.4271177968148,21.2116585821317,
16.6479889020655));
#201976=CARTESIAN_POINT('Ctrl Pts',(-19.3471103119782,21.2378262221791,
16.6534068325898));
#201977=CARTESIAN_POINT('Ctrl Pts',(-19.3016440361817,21.2510269091692,
16.6564042779727));
#201978=CARTESIAN_POINT('Ctrl Pts',(-19.2483037318369,21.2645919799044,
16.6597976700758));
#201979=CARTESIAN_POINT('Ctrl Pts',(-19.2408271465266,21.2664499741393,
16.6602705274235));
#201980=CARTESIAN_POINT('Ctrl Pts',(-19.2288395362173,21.2693596102613,
16.6610240447005));
#201981=CARTESIAN_POINT('Ctrl Pts',(-19.2243349937798,21.2704373130965,
16.6613061452149));
#201982=CARTESIAN_POINT('Ctrl Pts',(-19.2163364520529,21.2723232176344,
16.6618051608273));
#201983=CARTESIAN_POINT('Ctrl Pts',(-19.2128438940809,21.2731373345066,
16.6620224127647));
#201984=CARTESIAN_POINT('Ctrl Pts',(-19.2054208874389,21.2748477652032,
16.6624827774711));
#201985=CARTESIAN_POINT('Ctrl Pts',(-19.2014899512415,21.2757417265025,
16.6627257546235));
#201986=CARTESIAN_POINT('Ctrl Pts',(-19.1908386446496,21.2781320360373,
16.6633819839257));
#201987=CARTESIAN_POINT('Ctrl Pts',(-19.184113421763,21.279606852976,16.6637940182909));
#201988=CARTESIAN_POINT('Ctrl Pts',(-19.1502442975397,21.2868612357603,
16.6658580252429));
#201989=CARTESIAN_POINT('Ctrl Pts',(-19.1229944212617,21.292139758116,16.6674829968275));
#201990=CARTESIAN_POINT('Ctrl Pts',(-19.0432544637439,21.3059649611982,
16.6721551623251));
#201991=CARTESIAN_POINT('Ctrl Pts',(-18.9905343821223,21.3130721671704,
16.6751403830227));
#201992=CARTESIAN_POINT('Ctrl Pts',(-18.797470002405,21.331726311849,16.6858718161407));
#201993=CARTESIAN_POINT('Ctrl Pts',(-18.6563386417215,21.3312545783071,
16.6933556709626));
#201994=CARTESIAN_POINT('Ctrl Pts',(-18.4249190351338,21.3073293682037,
16.7062249140832));
#201995=CARTESIAN_POINT('Ctrl Pts',(-18.3342648253121,21.2919460974577,
16.7114159963734));
#201996=CARTESIAN_POINT('Ctrl Pts',(-18.2315114572506,21.2675465471129,
16.7176073324148));
#201997=CARTESIAN_POINT('Ctrl Pts',(-18.218151814816,21.2642362437222,16.7184182619345));
#201998=CARTESIAN_POINT('Ctrl Pts',(-18.1967880141909,21.2587209749307,
16.7197250009955));
#201999=CARTESIAN_POINT('Ctrl Pts',(-18.1887627598864,21.2565987528999,
16.7202181384911));
#202000=CARTESIAN_POINT('Ctrl Pts',(-18.1745411880844,21.2527483235335,
16.7210961367052));
#202001=CARTESIAN_POINT('Ctrl Pts',(-18.1683398432538,21.2510389615254,
16.7214803815956));
#202002=CARTESIAN_POINT('Ctrl Pts',(-18.1554407812215,21.2474200783434,
16.7222825707217));
#202003=CARTESIAN_POINT('Ctrl Pts',(-18.1487445125894,21.2455057182928,
16.7227006686577));
#202004=CARTESIAN_POINT('Ctrl Pts',(-18.1313907261432,21.2404517737632,
16.7237885635952));
#202005=CARTESIAN_POINT('Ctrl Pts',(-18.1207483627601,21.237261301269,16.724460015887));
#202006=CARTESIAN_POINT('Ctrl Pts',(-18.074747959663,21.2230752551771,16.7273812579463));
#202007=CARTESIAN_POINT('Ctrl Pts',(-18.0396584329149,21.2112373863709,
16.7296585095204));
#202008=CARTESIAN_POINT('Ctrl Pts',(-17.9473740482418,21.177383244029,16.7357823574816));
#202009=CARTESIAN_POINT('Ctrl Pts',(-17.8907970727781,21.1537946805069,
16.7396778781684));
#202010=CARTESIAN_POINT('Ctrl Pts',(-17.6945135637467,21.0617684287996,
16.7536785394432));
#202011=CARTESIAN_POINT('Ctrl Pts',(-17.5614180825771,20.98044103373,16.7641153034428));
#202012=CARTESIAN_POINT('Ctrl Pts',(-17.4260648076406,20.8757039401898,
16.7752422062864));
#202013=CARTESIAN_POINT('Ctrl Pts',(-17.4138001253349,20.8659942554115,
16.7762550795443));
#202014=CARTESIAN_POINT('Ctrl Pts',(-17.36384774033,20.8255393496894,16.7803961661011));
#202015=CARTESIAN_POINT('Ctrl Pts',(-17.3271142446875,20.793633187988,16.7834791138499));
#202016=CARTESIAN_POINT('Ctrl Pts',(-17.2858279037991,20.7551977985309,
16.7869573844483));
#202017=CARTESIAN_POINT('Ctrl Pts',(-17.2801751391209,20.7498770384019,
16.7874339089569));
#202018=CARTESIAN_POINT('Ctrl Pts',(-17.2711840645505,20.7413202773861,
16.7881921338877));
#202019=CARTESIAN_POINT('Ctrl Pts',(-17.2678269865608,20.7381042230305,
16.7884753028964));
#202020=CARTESIAN_POINT('Ctrl Pts',(-17.2618974317005,20.7323861788861,
16.7889755280837));
#202021=CARTESIAN_POINT('Ctrl Pts',(-17.2593206896836,20.7298886757621,
16.7891929268846));
#202022=CARTESIAN_POINT('Ctrl Pts',(-17.2538697539085,20.7245784176694,
16.7896528523257));
#202023=CARTESIAN_POINT('Ctrl Pts',(-17.2509972266505,20.7217640274666,
16.7898952471889));
#202024=CARTESIAN_POINT('Ctrl Pts',(-17.2432601359615,20.7141401969508,
16.7905482558267));
#202025=CARTESIAN_POINT('Ctrl Pts',(-17.2384107869143,20.7093152880961,
16.7909576721616));
#202026=CARTESIAN_POINT('Ctrl Pts',(-17.2143864470259,20.6851791761405,
16.7929871694037));
#202027=CARTESIAN_POINT('Ctrl Pts',(-17.1955607235697,20.6655220330636,
16.7945813190472));
#202028=CARTESIAN_POINT('Ctrl Pts',(-17.1421236884195,20.6075263719638,
16.7991369628542));
#202029=CARTESIAN_POINT('Ctrl Pts',(-17.1085281289397,20.5682759539064,
16.8020401077102));
#202030=CARTESIAN_POINT('Ctrl Pts',(-16.9906153898001,20.4198500712191,
16.8125410136528));
#202031=CARTESIAN_POINT('Ctrl Pts',(-16.9155865784353,20.303741249487,16.8198765234653));
#202032=CARTESIAN_POINT('Ctrl Pts',(-16.8441141284517,20.1651204890989,
16.8284838497148));
#202033=CARTESIAN_POINT('Ctrl Pts',(-16.8360514640181,20.1489796652897,
16.8294835060387));
#202034=CARTESIAN_POINT('Ctrl Pts',(-16.8183555773287,20.1123912973631,
16.8317463607716));
#202035=CARTESIAN_POINT('Ctrl Pts',(-16.80884162704,20.091888768662,16.8330121675465));
#202036=CARTESIAN_POINT('Ctrl Pts',(-16.7756490776912,20.0172516041905,
16.8376195413006));
#202037=CARTESIAN_POINT('Ctrl Pts',(-16.7539126431023,19.962287641449,16.8410121895392));
#202038=CARTESIAN_POINT('Ctrl Pts',(-16.7304860229088,19.8949373895622,
16.8452014435171));
#202039=CARTESIAN_POINT('Ctrl Pts',(-16.7265679215877,19.8833503925709,
16.8459232432515));
#202040=CARTESIAN_POINT('Ctrl Pts',(-16.7202764538486,19.8641992929252,
16.8471182860078));
#202041=CARTESIAN_POINT('Ctrl Pts',(-16.717844741408,19.8566545572059,16.8475896023454));
#202042=CARTESIAN_POINT('Ctrl Pts',(-16.7135348003855,19.8430205552864,
16.848442319599));
#202043=CARTESIAN_POINT('Ctrl Pts',(-16.7116415747875,19.8369361019763,
16.8488232222544));
#202044=CARTESIAN_POINT('Ctrl Pts',(-16.7076530215667,19.8239106705224,
16.8496394569432));
#202045=CARTESIAN_POINT('Ctrl Pts',(-16.7055658279232,19.8169673048608,
16.8500750499485));
#202046=CARTESIAN_POINT('Ctrl Pts',(-16.7000054583453,19.7981192287265,
16.8512588771066));
#202047=CARTESIAN_POINT('Ctrl Pts',(-16.696601192232,19.7861946384218,16.8520093477171));
#202048=CARTESIAN_POINT('Ctrl Pts',(-16.6796325708278,19.7247150385587,
16.8558867702653));
#202049=CARTESIAN_POINT('Ctrl Pts',(-16.6677716696659,19.6747115958207,
16.8590684023724));
#202050=CARTESIAN_POINT('Ctrl Pts',(-16.6242413884068,19.4560480100058,
16.8731123178568));
#202051=CARTESIAN_POINT('Ctrl Pts',(-16.6113283116054,19.2843350978315,
16.8845441214865));
#202052=CARTESIAN_POINT('Ctrl Pts',(-16.6234866307426,19.0220139847451,
16.9018091058584));
#202053=CARTESIAN_POINT('Ctrl Pts',(-16.633569184861,18.9313990754729,16.9077194382463));
#202054=CARTESIAN_POINT('Ctrl Pts',(-16.6511444198349,18.8321926861467,
16.9139439449464));
#202055=CARTESIAN_POINT('Ctrl Pts',(-16.6528949752438,18.822690544911,16.91453756761));
#202056=CARTESIAN_POINT('Ctrl Pts',(-16.6555773842658,18.8086696499825,
16.9154093505859));
#202057=CARTESIAN_POINT('Ctrl Pts',(-16.656459024255,18.8041415784687,16.9156902551318));
#202058=CARTESIAN_POINT('Ctrl Pts',(-16.6580501731279,18.7961095363258,
16.916187353207));
#202059=CARTESIAN_POINT('Ctrl Pts',(-16.6587537630014,18.7926044490709,
16.9164038794306));
#202060=CARTESIAN_POINT('Ctrl Pts',(-16.6602811653144,18.7850940063614,
16.9168669652411));
#202061=CARTESIAN_POINT('Ctrl Pts',(-16.6611077021402,18.7810892617399,
16.9171133671211));
#202062=CARTESIAN_POINT('Ctrl Pts',(-16.6634105741372,18.7700924158982,
16.9177885907733));
#202063=CARTESIAN_POINT('Ctrl Pts',(-16.6649107335244,18.7631052814737,
16.9182160718093));
#202064=CARTESIAN_POINT('Ctrl Pts',(-16.6731443930183,18.7256805779571,
16.9204981427327));
#202065=CARTESIAN_POINT('Ctrl Pts',(-16.6805145728341,18.6953852146079,
16.9223184367082));
#202066=CARTESIAN_POINT('Ctrl Pts',(-16.7307909376461,18.5069473644512,
16.933533356784));
#202067=CARTESIAN_POINT('Ctrl Pts',(-16.7912714468313,18.3540549666749,
16.9421917342362));
#202068=CARTESIAN_POINT('Ctrl Pts',(-16.9242256669935,18.1064001312441,
16.957577957569));
#202069=CARTESIAN_POINT('Ctrl Pts',(-16.9881305170594,18.0079378822575,
16.9641193305552));
#202070=CARTESIAN_POINT('Ctrl Pts',(-17.0685967551166,17.9039707846785,
16.9718211495755));
#202071=CARTESIAN_POINT('Ctrl Pts',(-17.077460019757,17.8927554791676,16.972662934909));
#202072=CARTESIAN_POINT('Ctrl Pts',(-17.0917460248004,17.8750500060118,
16.9740098757417));
#202073=CARTESIAN_POINT('Ctrl Pts',(-17.097095346178,17.8685009658746,16.9745120875452));
#202074=CARTESIAN_POINT('Ctrl Pts',(-17.1065983323504,17.8570079373491,
16.9754005945787));
#202075=CARTESIAN_POINT('Ctrl Pts',(-17.1107356726169,17.8520505470732,
16.9757862233266));
#202076=CARTESIAN_POINT('Ctrl Pts',(-17.1193394189939,17.8418368302834,
16.9765857189532));
#202077=CARTESIAN_POINT('Ctrl Pts',(-17.1238089593855,17.836583255291,16.9769997119573));
#202078=CARTESIAN_POINT('Ctrl Pts',(-17.1353465749404,17.8231552663939,
16.9780650371218));
#202079=CARTESIAN_POINT('Ctrl Pts',(-17.1424516467245,17.8150130335644,
16.9787178977584));
#202080=CARTESIAN_POINT('Ctrl Pts',(-17.1723582547554,17.7812659083372,
16.9814530342623));
#202081=CARTESIAN_POINT('Ctrl Pts',(-17.1957167391312,17.7561636151272,
16.9835586217593));
#202082=CARTESIAN_POINT('Ctrl Pts',(-17.2581508549208,17.6922537596297,
16.9891119975448));
#202083=CARTESIAN_POINT('Ctrl Pts',(-17.298147401795,17.6543859377552,16.9925981522907));
#202084=CARTESIAN_POINT('Ctrl Pts',(-17.4218565217009,17.5460891741164,
17.0031659000721));
#202085=CARTESIAN_POINT('Ctrl Pts',(-17.5095936082878,17.4805451213897,
17.010395889878));
#202086=CARTESIAN_POINT('Ctrl Pts',(-17.702130821921,17.3587100584198,17.0254469690628));
#202087=CARTESIAN_POINT('Ctrl Pts',(-17.8074254047905,17.3038560399,17.0332400120437));
#202088=CARTESIAN_POINT('Ctrl Pts',(-17.9255579694875,17.2544210289648,
17.0411497537052));
#202089=CARTESIAN_POINT('Ctrl Pts',(-17.934372513493,17.2508021331462,17.0417350723474));
#202090=CARTESIAN_POINT('Ctrl Pts',(-17.9474663139789,17.2455293690641,
17.0425970289135));
#202091=CARTESIAN_POINT('Ctrl Pts',(-17.9517268543673,17.2438297565147,
17.0428763242981));
#202092=CARTESIAN_POINT('Ctrl Pts',(-17.9593153269607,17.2408311190935,
17.0433716508496));
#202093=CARTESIAN_POINT('Ctrl Pts',(-17.9626410501634,17.2395266592974,
17.0435880057937));
#202094=CARTESIAN_POINT('Ctrl Pts',(-17.9697963453141,17.2367409914192,
17.0440519243042));
#202095=CARTESIAN_POINT('Ctrl Pts',(-17.9736269179161,17.2352625084545,
17.0442993238675));
#202096=CARTESIAN_POINT('Ctrl Pts',(-17.9842075399737,17.2312140433835,
17.0449801014598));
#202097=CARTESIAN_POINT('Ctrl Pts',(-17.990966550506,17.2286674185493,17.0454121018325));
#202098=CARTESIAN_POINT('Ctrl Pts',(-18.0279857950735,17.2149354408564,
17.047763107998));
#202099=CARTESIAN_POINT('Ctrl Pts',(-18.0584874180581,17.2044076673937,
17.049645318332));
#202100=CARTESIAN_POINT('Ctrl Pts',(-18.2443932449099,17.1449614850729,
17.0608552000322));
#202101=CARTESIAN_POINT('Ctrl Pts',(-18.4047918829387,17.1134147502264,
17.0694657658074));
#202102=CARTESIAN_POINT('Ctrl Pts',(-18.6837851614772,17.0913689021639,
17.0847864496237));
#202103=CARTESIAN_POINT('Ctrl Pts',(-18.8008813274884,17.0918305540773,
17.0913128877774));
#202104=CARTESIAN_POINT('Ctrl Pts',(-18.931569432224,17.1031908168632,17.09899789556));
#202105=CARTESIAN_POINT('Ctrl Pts',(-18.9457935912167,17.1045725284568,
17.0998394681574));
#202106=CARTESIAN_POINT('Ctrl Pts',(-18.9684091286237,17.1070007490587,
17.1011861321734));
#202107=CARTESIAN_POINT('Ctrl Pts',(-18.9768102631906,17.107953718895,17.1016882818113));
#202108=CARTESIAN_POINT('Ctrl Pts',(-18.9916166360501,17.1097231595595,
17.1025767164283));
#202109=CARTESIAN_POINT('Ctrl Pts',(-18.9980243057974,17.1105186609104,
17.102962335274));
#202110=CARTESIAN_POINT('Ctrl Pts',(-19.0112697208231,17.1122246225419,
17.1037618472599));
#202111=CARTESIAN_POINT('Ctrl Pts',(-19.0181068482672,17.1131392133591,
17.1041758667074));
#202112=CARTESIAN_POINT('Ctrl Pts',(-19.0356451191562,17.1155725871352,
17.1052413376107));
#202113=CARTESIAN_POINT('Ctrl Pts',(-19.0463392251379,17.1171399229768,
17.1058943183501));
#202114=CARTESIAN_POINT('Ctrl Pts',(-19.0909218854945,17.1240231306882,
17.1086306185752));
#202115=CARTESIAN_POINT('Ctrl Pts',(-19.1246891633661,17.1300801440805,
17.1107372745081));
#202116=CARTESIAN_POINT('Ctrl Pts',(-19.2122748455883,17.1479977764243,
17.1162941400135));
#202117=CARTESIAN_POINT('Ctrl Pts',(-19.2658010346737,17.1611434583797,
17.1197827761873));
#202118=CARTESIAN_POINT('Ctrl Pts',(-19.4264938850115,17.2073261803799,
17.1305297339397));
#202119=CARTESIAN_POINT('Ctrl Pts',(-19.5316004788073,17.2467987994143,
17.1379469158678));
#202120=CARTESIAN_POINT('Ctrl Pts',(-19.7377596912756,17.3435083559375,
17.1529857191004));
#202121=CARTESIAN_POINT('Ctrl Pts',(-19.8382546900748,17.4011142558444,
17.1605795851763));
#202122=CARTESIAN_POINT('Ctrl Pts',(-19.9414396663835,17.472072133917,17.1683151265274));
#202123=CARTESIAN_POINT('Ctrl Pts',(-19.9492920968202,17.477550895263,17.168903325603));
#202124=CARTESIAN_POINT('Ctrl Pts',(-19.9608585874898,17.4857382430863,
17.169768692267));
#202125=CARTESIAN_POINT('Ctrl Pts',(-19.964601304713,17.4884058651775,17.170048547271));
#202126=CARTESIAN_POINT('Ctrl Pts',(-19.971152957884,17.493107807014,17.1705381059388));
#202127=CARTESIAN_POINT('Ctrl Pts',(-19.9739656094503,17.4951368597897,
17.1707481665193));
#202128=CARTESIAN_POINT('Ctrl Pts',(-19.9767861316653,17.4971821476041,
17.1709587007979));
#202129=CARTESIAN_POINT('Ctrl Pts',(-19.976798940029,17.4971914357452,17.1709596568595));
#202130=CARTESIAN_POINT('Ctrl Pts',(-19.9768243308286,17.4972098486273,
17.1709615521142));
#202131=CARTESIAN_POINT('Ctrl Pts',(-19.976836913868,17.4972189737984,17.1709624913524));
#202132=CARTESIAN_POINT('Ctrl Pts',(-19.976861860772,17.4972370656151,17.1709643534645));
#202133=CARTESIAN_POINT('Ctrl Pts',(-19.9768742240742,17.4972460318455,
17.1709652762965));
#202134=CARTESIAN_POINT('Ctrl Pts',(-19.9768987356531,17.4972638087684,
17.1709671059062));
#202135=CARTESIAN_POINT('Ctrl Pts',(-19.9769108839021,17.4972726194336,
17.1709680126819));
#202136=CARTESIAN_POINT('Ctrl Pts',(-19.9769349703243,17.4972900887949,
17.1709698105485));
#202137=CARTESIAN_POINT('Ctrl Pts',(-19.9769469084253,17.4972987474319,
17.1709707016342));
#202138=CARTESIAN_POINT('Ctrl Pts',(-19.9769705784767,17.4973159155634,
17.1709724684141));
#202139=CARTESIAN_POINT('Ctrl Pts',(-19.976982310808,17.4973244253277,17.1709733441368));
#202140=CARTESIAN_POINT('Ctrl Pts',(-19.9770055739011,17.4973412990173,
17.1709750805329));
#202141=CARTESIAN_POINT('Ctrl Pts',(-19.9770171048129,17.4973496630452,
17.1709759412176));
#202142=CARTESIAN_POINT('Ctrl Pts',(-19.9770399705675,17.4973662492331,
17.1709776479483));
#202143=CARTESIAN_POINT('Ctrl Pts',(-19.9770513049473,17.4973744710512,
17.1709784939599));
#202144=CARTESIAN_POINT('Ctrl Pts',(-19.977073780378,17.4973907747896,17.1709801715493));
#202145=CARTESIAN_POINT('Ctrl Pts',(-19.9770849219528,17.497398857084,17.1709810031662));
#202146=CARTESIAN_POINT('Ctrl Pts',(-19.977107016468,17.497414885163,17.1709826523168));
#202147=CARTESIAN_POINT('Ctrl Pts',(-19.9771179693997,17.4974228309356,
17.1709834698499));
#202148=CARTESIAN_POINT('Ctrl Pts',(-19.9771396912811,17.4974385893296,
17.1709850911802));
#202149=CARTESIAN_POINT('Ctrl Pts',(-19.9771504598209,17.4974464016483,
17.1709858949469));
#202150=CARTESIAN_POINT('Ctrl Pts',(-19.9771718164569,17.4974618956853,
17.1709874890087));
#202151=CARTESIAN_POINT('Ctrl Pts',(-19.9771824044771,17.4974695773434,
17.1709882792982));
#202152=CARTESIAN_POINT('Ctrl Pts',(-19.9772034034501,17.4974848124934,
17.1709898466579));
#202153=CARTESIAN_POINT('Ctrl Pts',(-19.9772138145841,17.4974923661119,
17.1709906237416));
#202154=CARTESIAN_POINT('Ctrl Pts',(-19.9772339084215,17.4975069451281,
17.1709921235363));
#202155=CARTESIAN_POINT('Ctrl Pts',(-19.9772435910909,17.4975139704816,
17.1709928462449));
#202156=CARTESIAN_POINT('Ctrl Pts',(-19.97726291965,17.4975279947529,17.1709942889144));
#202157=CARTESIAN_POINT('Ctrl Pts',(-19.9772725657327,17.4975349938098,
17.1709950088896));
#202158=CARTESIAN_POINT('Ctrl Pts',(-19.977291821858,17.4975489660215,17.1709964461475));
#202159=CARTESIAN_POINT('Ctrl Pts',(-19.9773014317922,17.4975559390968,
17.1709971634221));
#202160=CARTESIAN_POINT('Ctrl Pts',(-19.977320616076,17.4975698596732,17.1709985953127));
#202161=CARTESIAN_POINT('Ctrl Pts',(-19.9773301903575,17.497576807124,17.1709993099237));
#202162=CARTESIAN_POINT('Ctrl Pts',(-19.9773493027676,17.4975906760362,
17.1710007364447));
#202163=CARTESIAN_POINT('Ctrl Pts',(-19.9773588413912,17.4975975978559,
17.1710014483916));
#202164=CARTESIAN_POINT('Ctrl Pts',(-19.9806629149965,17.4999952816906,
17.1712480585035));
#202165=CARTESIAN_POINT('Ctrl Pts',(-19.9839505796573,17.5023955639879,
17.171493293435));
#202166=CARTESIAN_POINT('Ctrl Pts',(-19.9907473935226,17.5073879486686,
17.1720000185021));
#202167=CARTESIAN_POINT('Ctrl Pts',(-19.9942554981795,17.5099814484733,
17.1722614116546));
#202168=CARTESIAN_POINT('Ctrl Pts',(-20.0031582711901,17.516605821497,17.1729244618015));
#202169=CARTESIAN_POINT('Ctrl Pts',(-20.0085418140649,17.5206516582818,
17.1733251233222));
#202170=CARTESIAN_POINT('Ctrl Pts',(-20.0240192051829,17.5323991994058,
17.1744764635561));
#202171=CARTESIAN_POINT('Ctrl Pts',(-20.0340633722757,17.5401662434556,
17.1752229672188));
#202172=CARTESIAN_POINT('Ctrl Pts',(-20.0683088146373,17.5671436564281,
17.1777681863004));
#202173=CARTESIAN_POINT('Ctrl Pts',(-20.0921600548039,17.5867939944063,
17.1795409393349));
#202174=CARTESIAN_POINT('Ctrl Pts',(-20.2113467482272,17.6894505634705,
17.188449062742));
#202175=CARTESIAN_POINT('Ctrl Pts',(-20.299546724616,17.7803586925282,17.1952196583335));
#202176=CARTESIAN_POINT('Ctrl Pts',(-20.4097844625949,17.9164690961939,
17.2047555495432));
#202177=CARTESIAN_POINT('Ctrl Pts',(-20.43913807349,17.9553855091922,17.2074206101436));
#202178=CARTESIAN_POINT('Ctrl Pts',(-20.5189778804002,18.0692045004508,
17.2151169900671));
#202179=CARTESIAN_POINT('Ctrl Pts',(-20.5660451944649,18.1463636602338,
17.2202235061175));
#202180=CARTESIAN_POINT('Ctrl Pts',(-20.614423582134,18.2384340743941,17.2263211557695));
#202181=CARTESIAN_POINT('Ctrl Pts',(-20.6206885111512,18.2506439324104,
17.2271297421923));
#202182=CARTESIAN_POINT('Ctrl Pts',(-20.6305464904218,18.2703251773399,
17.2284334242447));
#202183=CARTESIAN_POINT('Ctrl Pts',(-20.6342151974782,18.2777583846572,
17.2289258679561));
#202184=CARTESIAN_POINT('Ctrl Pts',(-20.6406524019749,18.2909962097609,
17.2298030681659));
#202185=CARTESIAN_POINT('Ctrl Pts',(-20.6434382975264,18.2967922869821,
17.2301872126918));
#202186=CARTESIAN_POINT('Ctrl Pts',(-20.6491885396076,18.3088966582987,
17.2309896346162));
#202187=CARTESIAN_POINT('Ctrl Pts',(-20.6521482233075,18.3152070702627,
17.2314080679141));
#202188=CARTESIAN_POINT('Ctrl Pts',(-20.6597551194754,18.3316364746616,
17.2324978029263));
#202189=CARTESIAN_POINT('Ctrl Pts',(-20.6643537093322,18.3417776237763,
17.23317077043));
#202190=CARTESIAN_POINT('Ctrl Pts',(-20.6839918006411,18.3860094952924,
17.2361077301152));
#202191=CARTESIAN_POINT('Ctrl Pts',(-20.6982090530658,18.4204559628926,
17.2383995513923));
#202192=CARTESIAN_POINT('Ctrl Pts',(-20.7335762447422,18.5129993850948,
17.2445727474128));
#202193=CARTESIAN_POINT('Ctrl Pts',(-20.7531018231504,18.5716747977174,
17.2485040294199));
#202194=CARTESIAN_POINT('Ctrl Pts',(-20.8238088869656,18.8199345232613,
17.265181550711));
#202195=CARTESIAN_POINT('Ctrl Pts',(-20.8510531407969,19.015286332678,17.2785154521607));
#202196=CARTESIAN_POINT('Ctrl Pts',(-20.8509999221906,19.2115739728967,
17.290908287241));
#202197=CARTESIAN_POINT('Ctrl Pts',(-20.8509999215533,19.211576318847,17.2909084353551));
#202198=CARTESIAN_POINT('Ctrl Pts',(-20.8509956361944,19.2273177864368,
17.2919022894384));
#202199=CARTESIAN_POINT('Ctrl Pts',(-20.8508157764495,19.2430592819062,
17.2928890187188));
#202200=CARTESIAN_POINT('Ctrl Pts',(-20.8502148553261,19.2696677093326,
17.294543265343));
#202201=CARTESIAN_POINT('Ctrl Pts',(-20.8498856305801,19.2805357712956,
17.295215078138));
#202202=CARTESIAN_POINT('Ctrl Pts',(-20.8492914997326,19.2961682450766,
17.2961753949309));
#202203=CARTESIAN_POINT('Ctrl Pts',(-20.8490942018497,19.3009348492606,
17.2964674073038));
#202204=CARTESIAN_POINT('Ctrl Pts',(-20.8487208813595,19.3092719314371,
17.296976699464));
#202205=CARTESIAN_POINT('Ctrl Pts',(-20.8485519257252,19.3128426846232,
17.2971943609584));
#202206=CARTESIAN_POINT('Ctrl Pts',(-20.8482044716738,19.3198119163801,
17.2976182479406));
#202207=CARTESIAN_POINT('Ctrl Pts',(-20.8480268210971,19.3232104340723,
17.2978245201538));
#202208=CARTESIAN_POINT('Ctrl Pts',(-20.8476550551564,19.3300079760932,
17.2982362092455));
#202209=CARTESIAN_POINT('Ctrl Pts',(-20.8474609356904,19.3334069616119,
17.2984416261313));
#202210=CARTESIAN_POINT('Ctrl Pts',(-20.8469736811295,19.3415917783836,
17.2989352437825));
#202211=CARTESIAN_POINT('Ctrl Pts',(-20.8466724833011,19.3463771363713,
17.299222995435));
#202212=CARTESIAN_POINT('Ctrl Pts',(-20.8455076184958,19.3639326585952,
17.3002756599104));
#202213=CARTESIAN_POINT('Ctrl Pts',(-20.8445443836754,19.3766962389897,
17.3010352044386));
#202214=CARTESIAN_POINT('Ctrl Pts',(-20.8412948234941,19.415109295813,17.303305779114));
#202215=CARTESIAN_POINT('Ctrl Pts',(-20.8386561520336,19.440727409303,17.3047994319179));
#202216=CARTESIAN_POINT('Ctrl Pts',(-20.8160117669933,19.6271347049876,
17.3155582884879));
#202217=CARTESIAN_POINT('Ctrl Pts',(-20.7780853950748,19.7851006901587,
17.3241154224325));
#202218=CARTESIAN_POINT('Ctrl Pts',(-20.7225806054527,19.9371103054064,
17.3329786569753));
#202219=CARTESIAN_POINT('Origin',(-18.734,19.211,0.));
#202220=CARTESIAN_POINT('',(-20.7225806168679,19.9371102741439,18.3568545763217));
#202221=CARTESIAN_POINT('',(-20.7225805905512,19.9371103462167,18.1318063719887));
#202222=CARTESIAN_POINT('',(-20.7225806064498,19.9371103026755,0.));
#202223=CARTESIAN_POINT('Ctrl Pts',(-20.7225806168679,19.9371102741439,
18.3568545763217));
#202224=CARTESIAN_POINT('Ctrl Pts',(-20.7279235886306,19.9224776068176,
18.3558520750571));
#202225=CARTESIAN_POINT('Ctrl Pts',(-20.7331056671166,19.9077842824243,
18.3548454788278));
#202226=CARTESIAN_POINT('Ctrl Pts',(-20.7819939765922,19.7641279866657,
18.3450068771352));
#202227=CARTESIAN_POINT('Ctrl Pts',(-20.8133220094845,19.6312931103634,
18.3359031763939));
#202228=CARTESIAN_POINT('Ctrl Pts',(-20.8417530898284,19.4223144011233,
18.3221216513367));
#202229=CARTESIAN_POINT('Ctrl Pts',(-20.8479010440638,19.3477542444381,
18.3173148433635));
#202230=CARTESIAN_POINT('Ctrl Pts',(-20.8503509135829,19.2641628324461,
18.3121557836362));
#202231=CARTESIAN_POINT('Ctrl Pts',(-20.8505548516267,19.2553062358344,
18.311612076797));
#202232=CARTESIAN_POINT('Ctrl Pts',(-20.8507777608051,19.2419958471638,
18.3107995733725));
#202233=CARTESIAN_POINT('Ctrl Pts',(-20.8508382796755,19.2375429787264,
18.3105285349334));
#202234=CARTESIAN_POINT('Ctrl Pts',(-20.8509183443716,19.229870345947,18.3100628926518));
#202235=CARTESIAN_POINT('Ctrl Pts',(-20.8509445960013,19.2266507069947,
18.3098679164559));
#202236=CARTESIAN_POINT('Ctrl Pts',(-20.8509874023438,19.2193608829985,
18.3094274124076));
#202237=CARTESIAN_POINT('Ctrl Pts',(-20.8509995645905,19.2152907123876,
18.3091821332973));
#202238=CARTESIAN_POINT('Ctrl Pts',(-20.8510007238756,19.2041601518444,
18.3085131479209));
#202239=CARTESIAN_POINT('Ctrl Pts',(-20.8509661391565,19.1970997382133,
18.3080907414477));
#202240=CARTESIAN_POINT('Ctrl Pts',(-20.8505991940029,19.1600402483695,
18.3058831832676));
#202241=CARTESIAN_POINT('Ctrl Pts',(-20.8496644764733,19.1300489297337,
18.3041297304724));
#202242=CARTESIAN_POINT('Ctrl Pts',(-20.8449576379443,19.04033360736,18.2989567920898));
#202243=CARTESIAN_POINT('Ctrl Pts',(-20.8392907053301,18.9807365831336,
18.2956162060616));
#202244=CARTESIAN_POINT('Ctrl Pts',(-20.8082534041835,18.7559400892342,
18.2831217032851));
#202245=CARTESIAN_POINT('Ctrl Pts',(-20.7658882389287,18.5937173192297,
18.2742743496021));
#202246=CARTESIAN_POINT('Ctrl Pts',(-20.6832635060479,18.3830083038489,
18.2615098046473));
#202247=CARTESIAN_POINT('Ctrl Pts',(-20.6593330779176,18.3287924993762,
18.2581084530173));
#202248=CARTESIAN_POINT('Ctrl Pts',(-20.6277538502301,18.264672779265,18.2539094981777));
#202249=CARTESIAN_POINT('Ctrl Pts',(-20.6222501813624,18.2537382295761,
18.2531871161297));
#202250=CARTESIAN_POINT('Ctrl Pts',(-20.6130255038378,18.2357999992725,
18.2519913061925));
#202251=CARTESIAN_POINT('Ctrl Pts',(-20.6093593760602,18.2287683096653,
18.2515198093162));
#202252=CARTESIAN_POINT('Ctrl Pts',(-20.6026761040452,18.2161235119061,
18.2506668971066));
#202253=CARTESIAN_POINT('Ctrl Pts',(-20.5996729454112,18.2105030895702,
18.2502859810478));
#202254=CARTESIAN_POINT('Ctrl Pts',(-20.5931997793556,18.1985190289402,
18.2494698618593));
#202255=CARTESIAN_POINT('Ctrl Pts',(-20.5897223818567,18.1921594944472,
18.2490343985108));
#202256=CARTESIAN_POINT('Ctrl Pts',(-20.5802117614021,18.1749765069678,
18.2478512849531));
#202257=CARTESIAN_POINT('Ctrl Pts',(-20.5741161268356,18.1641880896839,
18.2471014028714));
#202258=CARTESIAN_POINT('Ctrl Pts',(-20.5423238602427,18.1090560473854,
18.243232325567));
#202259=CARTESIAN_POINT('Ctrl Pts',(-20.5151196159157,18.0656058060472,
18.2400587313911));
#202260=CARTESIAN_POINT('Ctrl Pts',(-20.3905640768228,17.8818502138373,
18.2260767525442));
#202261=CARTESIAN_POINT('Ctrl Pts',(-20.2780223785624,17.7526372262008,
18.2147048635678));
#202262=CARTESIAN_POINT('Ctrl Pts',(-20.082846824392,17.5767503536245,18.1974265663112));
#202263=CARTESIAN_POINT('Ctrl Pts',(-20.0105229808749,17.5196535766864,
18.1914504713804));
#202264=CARTESIAN_POINT('Ctrl Pts',(-19.9267413463558,17.4619572449719,
18.1851656487334));
#202265=CARTESIAN_POINT('Ctrl Pts',(-19.9187408031815,17.4565280806922,
18.1845716097907));
#202266=CARTESIAN_POINT('Ctrl Pts',(-19.9068673061104,17.4485889882307,
18.1836993345904));
#202267=CARTESIAN_POINT('Ctrl Pts',(-19.9030230211864,17.4460366947114,
18.1834183497158));
#202268=CARTESIAN_POINT('Ctrl Pts',(-19.8961854772461,17.4415292604913,
18.1829211629406));
#202269=CARTESIAN_POINT('Ctrl Pts',(-19.8931955833309,17.4395691145963,
18.1827046279009));
#202270=CARTESIAN_POINT('Ctrl Pts',(-19.8867759743441,17.4353836937622,
18.1822415824304));
#202271=CARTESIAN_POINT('Ctrl Pts',(-19.8833447842729,17.433160782996,18.1819952293969));
#202272=CARTESIAN_POINT('Ctrl Pts',(-19.873901494864,17.4270816731741,18.1813202773879));
#202273=CARTESIAN_POINT('Ctrl Pts',(-19.8678762220928,17.4232458974844,
18.1808930173543));
#202274=CARTESIAN_POINT('Ctrl Pts',(-19.8354945546945,17.4028608257797,
18.1786142538754));
#202275=CARTESIAN_POINT('Ctrl Pts',(-19.8087935695442,17.3868627953459,
18.176796928762));
#202276=CARTESIAN_POINT('Ctrl Pts',(-19.639330541107,17.2903417119676,18.1655817188541));
#202277=CARTESIAN_POINT('Ctrl Pts',(-19.4879598292091,17.2260293189489,
18.1569210140017));
#202278=CARTESIAN_POINT('Ctrl Pts',(-19.2182121069083,17.1467893281181,
18.1415316377863));
#202279=CARTESIAN_POINT('Ctrl Pts',(-19.1032202690765,17.1231546613371,
18.1349895793114));
#202280=CARTESIAN_POINT('Ctrl Pts',(-18.9726799019284,17.1074493714411,
18.1272869887103));
#202281=CARTESIAN_POINT('Ctrl Pts',(-18.958470743088,17.1058857007117,18.1264451937821));
#202282=CARTESIAN_POINT('Ctrl Pts',(-18.9358327578082,17.1036262685085,
18.1250982404687));
#202283=CARTESIAN_POINT('Ctrl Pts',(-18.9274135620935,17.1028368902909,
18.1245960258657));
#202284=CARTESIAN_POINT('Ctrl Pts',(-18.912557589538,17.1015337450178,18.123707515576));
#202285=CARTESIAN_POINT('Ctrl Pts',(-18.9061227320673,17.1009989437514,
18.1233218863871));
#202286=CARTESIAN_POINT('Ctrl Pts',(-18.892809139967,17.0999537584515,18.1225223915118));
#202287=CARTESIAN_POINT('Ctrl Pts',(-18.8859301638656,17.0994475378411,
18.1221083997082));
#202288=CARTESIAN_POINT('Ctrl Pts',(-18.8682679935417,17.098234541639,18.1210430811407));
#202289=CARTESIAN_POINT('Ctrl Pts',(-18.8574817370218,17.0975767035508,
18.1203902259372));
#202290=CARTESIAN_POINT('Ctrl Pts',(-18.8124546918413,17.095176443615,18.117655142007));
#202291=CARTESIAN_POINT('Ctrl Pts',(-18.7781807231669,17.0941834495625,
18.1155496027715));
#202292=CARTESIAN_POINT('Ctrl Pts',(-18.688839404307,17.0937656779543,18.1099963845837));
#202293=CARTESIAN_POINT('Ctrl Pts',(-18.6337945776069,17.0956563616929,
18.1065103418884));
#202294=CARTESIAN_POINT('Ctrl Pts',(-18.4698250798929,17.1077026203323,
18.0959428093823));
#202295=CARTESIAN_POINT('Ctrl Pts',(-18.3615528642482,17.1241535945483,
18.088712922088));
#202296=CARTESIAN_POINT('Ctrl Pts',(-18.2114893144157,17.1590080248056,
18.0785361845688));
#202297=CARTESIAN_POINT('Ctrl Pts',(-18.1682636355976,17.1705022604532,
18.0755877053219));
#202298=CARTESIAN_POINT('Ctrl Pts',(-18.1012764327963,17.1906074579972,
18.0710174114961));
#202299=CARTESIAN_POINT('Ctrl Pts',(-18.077250090143,17.1982892003561,18.0693780401148));
#202300=CARTESIAN_POINT('Ctrl Pts',(-18.006137231317,17.2224345601641,18.0645356450814));
#202301=CARTESIAN_POINT('Ctrl Pts',(-17.9594855135928,17.2401360028084,
18.061371658143));
#202302=CARTESIAN_POINT('Ctrl Pts',(-17.9062948296633,17.2624994930913,
18.0578132726379));
#202303=CARTESIAN_POINT('Ctrl Pts',(-17.8991073595939,17.2655683364015,
18.0573335036114));
#202304=CARTESIAN_POINT('Ctrl Pts',(-17.8876575865571,17.2705322023204,
18.0565711162539));
#202305=CARTESIAN_POINT('Ctrl Pts',(-17.8833843460532,17.2724015978434,
18.056287004365));
#202306=CARTESIAN_POINT('Ctrl Pts',(-17.875832536487,17.275735032019,18.0557857086616));
#202307=CARTESIAN_POINT('Ctrl Pts',(-17.8725514708351,17.2771933074717,
18.055568177123));
#202308=CARTESIAN_POINT('Ctrl Pts',(-17.865611165972,17.2802991074329,18.0551086247204));
#202309=CARTESIAN_POINT('Ctrl Pts',(-17.8619529037576,17.2819486875214,
18.0548667322983));
#202310=CARTESIAN_POINT('Ctrl Pts',(-17.8521061472497,17.2864225124618,
18.054216501074));
#202311=CARTESIAN_POINT('Ctrl Pts',(-17.8459264774879,17.2892662269344,
18.0538093422824));
#202312=CARTESIAN_POINT('Ctrl Pts',(-17.8155064714923,17.3034427516473,
18.0518090780955));
#202313=CARTESIAN_POINT('Ctrl Pts',(-17.7914676120732,17.3152052151806,
18.0502410158005));
#202314=CARTESIAN_POINT('Ctrl Pts',(-17.7228425003853,17.3504123358398,
18.0457829537353));
#202315=CARTESIAN_POINT('Ctrl Pts',(-17.678859712758,17.3749973867461,18.0429483593201));
#202316=CARTESIAN_POINT('Ctrl Pts',(-17.5228519653038,17.4696609479272,
18.0328288287506));
#202317=CARTESIAN_POINT('Ctrl Pts',(-17.4165711005165,17.5486147279255,
18.0257912722745));
#202318=CARTESIAN_POINT('Ctrl Pts',(-17.2410480228008,17.7064769250663,
18.0128047330271));
#202319=CARTESIAN_POINT('Ctrl Pts',(-17.1689908609921,17.7815813626763,
18.0069646491463));
#202320=CARTESIAN_POINT('Ctrl Pts',(-17.0937851868561,17.8725000941801,
18.0000501723039));
#202321=CARTESIAN_POINT('Ctrl Pts',(-17.0849331101857,17.8834213733836,
17.9992221269926));
#202322=CARTESIAN_POINT('Ctrl Pts',(-17.0709745037462,17.9009978831344,
17.9978930751351));
#202323=CARTESIAN_POINT('Ctrl Pts',(-17.0657975265354,17.9075968191615,
17.9973948898039));
#202324=CARTESIAN_POINT('Ctrl Pts',(-17.0567114623928,17.9193213588089,
17.9965110615274));
#202325=CARTESIAN_POINT('Ctrl Pts',(-17.0527862941115,17.9244344073417,
17.9961260625336));
#202326=CARTESIAN_POINT('Ctrl Pts',(-17.0446920345478,17.9350785402328,
17.9953254495193));
#202327=CARTESIAN_POINT('Ctrl Pts',(-17.0405266188825,17.9406123114154,
17.9949096973999));
#202328=CARTESIAN_POINT('Ctrl Pts',(-17.0298540954973,17.9549365658835,
17.9938346880525));
#202329=CARTESIAN_POINT('Ctrl Pts',(-17.0233878775954,17.9637571311048,
17.9931738483764));
#202330=CARTESIAN_POINT('Ctrl Pts',(-16.9962601444118,18.0013698608516,
17.9903603332824));
#202331=CARTESIAN_POINT('Ctrl Pts',(-16.9762559466372,18.0306269726025,
17.9881826429289));
#202332=CARTESIAN_POINT('Ctrl Pts',(-16.9256702920182,18.1087502383496,
17.9823920771855));
#202333=CARTESIAN_POINT('Ctrl Pts',(-16.8963354105636,18.1583847826659,
17.9787366240366));
#202334=CARTESIAN_POINT('Ctrl Pts',(-16.7931942183012,18.3503815039853,
17.9646995012915));
#202335=CARTESIAN_POINT('Ctrl Pts',(-16.7336208999361,18.4997564510137,
17.9539364305487));
#202336=CARTESIAN_POINT('Ctrl Pts',(-16.6877207719693,18.6681976139541,
17.9425813488462));
#202337=CARTESIAN_POINT('Ctrl Pts',(-16.68410418427,18.6820195959151,17.9416554963001));
#202338=CARTESIAN_POINT('Ctrl Pts',(-16.6785657088547,18.7040969632575,
17.9401870890761));
#202339=CARTESIAN_POINT('Ctrl Pts',(-16.6765530321099,18.712328974593,17.9396418592465));
#202340=CARTESIAN_POINT('Ctrl Pts',(-16.6646682505495,18.762235764839,17.9363511025041));
#202341=CARTESIAN_POINT('Ctrl Pts',(-16.6560124564913,18.804193448197,17.9336463329712));
#202342=CARTESIAN_POINT('Ctrl Pts',(-16.6473466573013,18.8537566855506,
17.930545618189));
#202343=CARTESIAN_POINT('Ctrl Pts',(-16.6460973255535,18.8611323333694,
17.9300866318769));
#202344=CARTESIAN_POINT('Ctrl Pts',(-16.6441405110127,18.8730686266629,
17.9293479491722));
#202345=CARTESIAN_POINT('Ctrl Pts',(-16.6434088124107,18.877625159766,17.9290669332108));
#202346=CARTESIAN_POINT('Ctrl Pts',(-16.6421367095041,18.8857158845745,
17.9285697121013));
#202347=CARTESIAN_POINT('Ctrl Pts',(-16.6415903529058,18.8892490850111,
17.928353173642));
#202348=CARTESIAN_POINT('Ctrl Pts',(-16.6404384571288,18.8968252435236,
17.9278901437483));
#202349=CARTESIAN_POINT('Ctrl Pts',(-16.6398356785746,18.9008685650967,
17.9276438095914));
#202350=CARTESIAN_POINT('Ctrl Pts',(-16.638212126157,18.9119796294738,17.9269689625562));
#202351=CARTESIAN_POINT('Ctrl Pts',(-16.6372153844792,18.9190509058753,
17.9265417879267));
#202352=CARTESIAN_POINT('Ctrl Pts',(-16.6320693322199,18.9569453925563,
17.9242643010476));
#202353=CARTESIAN_POINT('Ctrl Pts',(-16.6285636239004,18.9878539208088,
17.9224481218038));
#202354=CARTESIAN_POINT('Ctrl Pts',(-16.6108607051316,19.1820694907886,
17.9112327987635));
#202355=CARTESIAN_POINT('Ctrl Pts',(-16.6149886575892,19.3465018782596,
17.9025711946963));
#202356=CARTESIAN_POINT('Ctrl Pts',(-16.6545441347814,19.6248738248299,
17.8871806013251));
#202357=CARTESIAN_POINT('Ctrl Pts',(-16.6806410937662,19.7393371488572,
17.880638279104));
#202358=CARTESIAN_POINT('Ctrl Pts',(-16.7203942459428,19.8646705680541,
17.8729353916303));
#202359=CARTESIAN_POINT('Ctrl Pts',(-16.7248539255653,19.878252112002,17.8720935930106));
#202360=CARTESIAN_POINT('Ctrl Pts',(-16.7321700699384,19.8997941911237,
17.8707466348939));
#202361=CARTESIAN_POINT('Ctrl Pts',(-16.7349373303762,19.9077847202459,
17.8702444192122));
#202362=CARTESIAN_POINT('Ctrl Pts',(-16.7399019451138,19.9218471292961,
17.8693559076657));
#202363=CARTESIAN_POINT('Ctrl Pts',(-16.7420793578828,19.9279259709419,
17.8689702783047));
#202364=CARTESIAN_POINT('Ctrl Pts',(-16.7466401843047,19.9404775800184,
17.8681707837129));
#202365=CARTESIAN_POINT('Ctrl Pts',(-16.7490274876515,19.9469488435071,
17.8677567923678));
#202366=CARTESIAN_POINT('Ctrl Pts',(-16.755235989049,19.9635282482156,17.8666914763274));
#202367=CARTESIAN_POINT('Ctrl Pts',(-16.7591030005804,19.9736189155141,
17.8660386232066));
#202368=CARTESIAN_POINT('Ctrl Pts',(-16.7755605404946,20.0155988587882,
17.863303559453));
#202369=CARTESIAN_POINT('Ctrl Pts',(-16.7888469702367,20.0472080572438,
17.8611980387414));
#202370=CARTESIAN_POINT('Ctrl Pts',(-16.8254562142462,20.128704309467,17.8556448810496));
#202371=CARTESIAN_POINT('Ctrl Pts',(-16.8499670865737,20.1780262374202,
17.8521588813683));
#202372=CARTESIAN_POINT('Ctrl Pts',(-16.9288198107064,20.3222932200393,
17.8415914314985));
#202373=CARTESIAN_POINT('Ctrl Pts',(-16.988621974948,20.4140379127527,17.834361583553));
#202374=CARTESIAN_POINT('Ctrl Pts',(-17.0824452229109,20.5361605065567,
17.8241885267367));
#202375=CARTESIAN_POINT('Ctrl Pts',(-17.110768268272,20.5707067589978,17.8212436790553));
#202376=CARTESIAN_POINT('Ctrl Pts',(-17.1568585388308,20.6234295589014,
17.8166674393319));
#202377=CARTESIAN_POINT('Ctrl Pts',(-17.1738960661287,20.6422261299244,
17.8150186759653));
#202378=CARTESIAN_POINT('Ctrl Pts',(-17.2253673726505,20.6970000573184,
17.8101725035341));
#202379=CARTESIAN_POINT('Ctrl Pts',(-17.2607397999422,20.7320765333519,
17.8070138580573));
#202380=CARTESIAN_POINT('Ctrl Pts',(-17.3030568212839,20.7711767980069,
17.8034607457834));
#202381=CARTESIAN_POINT('Ctrl Pts',(-17.3088236473285,20.7764463867677,
17.8029811862584));
#202382=CARTESIAN_POINT('Ctrl Pts',(-17.3180794188717,20.7848105519321,
17.8022190675972));
#202383=CARTESIAN_POINT('Ctrl Pts',(-17.3215495863083,20.7879256720775,
17.801935016521));
#202384=CARTESIAN_POINT('Ctrl Pts',(-17.3277097403663,20.7934189067434,
17.8014337899495));
#202385=CARTESIAN_POINT('Ctrl Pts',(-17.3303955184644,20.7958016755775,
17.8012162670592));
#202386=CARTESIAN_POINT('Ctrl Pts',(-17.3360964234948,20.8008335443592,
17.8007566910019));
#202387=CARTESIAN_POINT('Ctrl Pts',(-17.3391130195072,20.803480901061,17.8005147664904));
#202388=CARTESIAN_POINT('Ctrl Pts',(-17.3472644947487,20.8105936811273,
17.7998643579212));
#202389=CARTESIAN_POINT('Ctrl Pts',(-17.3524134562302,20.8150429954258,
17.7994570549838));
#202390=CARTESIAN_POINT('Ctrl Pts',(-17.3779365132596,20.836883876991,17.7974549385015));
#202391=CARTESIAN_POINT('Ctrl Pts',(-17.3986189788513,20.8539133395081,
17.795885223844));
#202392=CARTESIAN_POINT('Ctrl Pts',(-17.4591673799483,20.9018683658375,
17.7914210089148));
#202393=CARTESIAN_POINT('Ctrl Pts',(-17.4998242932351,20.9317687362996,
17.7885820971808));
#202394=CARTESIAN_POINT('Ctrl Pts',(-17.653842795072,21.0367687972392,17.7782457286038));
#202395=CARTESIAN_POINT('Ctrl Pts',(-17.7732895619697,21.1023511818719,
17.7710112720879));
#202396=CARTESIAN_POINT('Ctrl Pts',(-17.9902203303781,21.1955682718228,
17.7580012076775));
#202397=CARTESIAN_POINT('Ctrl Pts',(-18.0849153183013,21.2285244231646,
17.7523642927888));
#202398=CARTESIAN_POINT('Ctrl Pts',(-18.1950693905495,21.2583001903951,
17.7456767073605));
#202399=CARTESIAN_POINT('Ctrl Pts',(-18.2085947232566,21.2618129004394,
17.7448535528168));
#202400=CARTESIAN_POINT('Ctrl Pts',(-18.2302682573637,21.2672133321497,
17.7435308735146));
#202401=CARTESIAN_POINT('Ctrl Pts',(-18.2383947298294,21.2691871511032,
17.7430341269616));
#202402=CARTESIAN_POINT('Ctrl Pts',(-18.2528015878765,21.2725961265103,
17.7421519645916));
#202403=CARTESIAN_POINT('Ctrl Pts',(-18.2590772636499,21.2740508703748,
17.7417671846968));
#202404=CARTESIAN_POINT('Ctrl Pts',(-18.2721242579922,21.2770125653109,
17.7409661429812));
#202405=CARTESIAN_POINT('Ctrl Pts',(-18.2788965307704,21.2785149217335,
17.740549738684));
#202406=CARTESIAN_POINT('Ctrl Pts',(-18.2964119598141,21.2823103050414,
17.7394711440535));
#202407=CARTESIAN_POINT('Ctrl Pts',(-18.3071656985573,21.2845530243213,
17.7388073511231));
#202408=CARTESIAN_POINT('Ctrl Pts',(-18.3531107373858,21.2937624261987,
17.7359642653186));
#202409=CARTESIAN_POINT('Ctrl Pts',(-18.3884569324463,21.2999173501348,
17.7337592980743));
#202410=CARTESIAN_POINT('Ctrl Pts',(-18.4819311258842,21.3137569704982,
17.7278780969134));
#202411=CARTESIAN_POINT('Ctrl Pts',(-18.5402484715471,21.3199298147708,
17.7241576093364));
#202412=CARTESIAN_POINT('Ctrl Pts',(-18.7473246243964,21.3331871926574,
17.7107831679876));
#202413=CARTESIAN_POINT('Ctrl Pts',(-18.8964911736824,21.3269977588632,
17.7008169090588));
#202414=CARTESIAN_POINT('Ctrl Pts',(-19.0680941647076,21.3016160512741,
17.6894824109724));
#202415=CARTESIAN_POINT('Ctrl Pts',(-19.0923699971672,21.2975918133585,
17.6878831494053));
#202416=CARTESIAN_POINT('Ctrl Pts',(-19.1336879945986,21.2900000956134,
17.6851737561915));
#202417=CARTESIAN_POINT('Ctrl Pts',(-19.1507662212408,21.2866439575585,
17.6840575710416));
#202418=CARTESIAN_POINT('Ctrl Pts',(-19.2014517908399,21.2760326371987,
17.68075953865));
#202419=CARTESIAN_POINT('Ctrl Pts',(-19.234927723046,21.2681686119622,17.6786005102154));
#202420=CARTESIAN_POINT('Ctrl Pts',(-19.2749606341334,21.2577289552398,
17.6760537072737));
#202421=CARTESIAN_POINT('Ctrl Pts',(-19.281713263303,21.2559322747254,17.6756253352694));
#202422=CARTESIAN_POINT('Ctrl Pts',(-19.2927662000449,21.2529327292171,
17.6749262962257));
#202423=CARTESIAN_POINT('Ctrl Pts',(-19.2970717556372,21.2517496504495,
17.6746545255179));
#202424=CARTESIAN_POINT('Ctrl Pts',(-19.3048060212234,21.2495980917104,
17.6741673305775));
#202425=CARTESIAN_POINT('Ctrl Pts',(-19.3082360407309,21.2486345755521,
17.6739516244455));
#202426=CARTESIAN_POINT('Ctrl Pts',(-19.3156983919501,21.2465180100373,
17.6734831149007));
#202427=CARTESIAN_POINT('Ctrl Pts',(-19.3197297216952,21.2453616399762,
17.6732305075531));
#202428=CARTESIAN_POINT('Ctrl Pts',(-19.3310810019851,21.2420690341085,
17.6725205431446));
#202429=CARTESIAN_POINT('Ctrl Pts',(-19.3383929711427,21.2399051936171,
17.672064765109));
#202430=CARTESIAN_POINT('Ctrl Pts',(-19.3828137042124,21.2264982581414,
17.6693044194649));
#202431=CARTESIAN_POINT('Ctrl Pts',(-19.4196220666681,21.2142761319886,
17.667053425374));
#202432=CARTESIAN_POINT('Ctrl Pts',(-19.6072900349678,21.1461820192928,
17.6556662031394));
#202433=CARTESIAN_POINT('Ctrl Pts',(-19.7517706429219,21.0742546919518,
17.6471669127988));
#202434=CARTESIAN_POINT('Ctrl Pts',(-19.9805519550366,20.9257338806469,
17.6322084729279));
#202435=CARTESIAN_POINT('Ctrl Pts',(-20.0693962758234,20.8574859732337,
17.6259478962023));
#202436=CARTESIAN_POINT('Ctrl Pts',(-20.1629762519826,20.7730236270999,
17.618562114518));
#202437=CARTESIAN_POINT('Ctrl Pts',(-20.1734290681947,20.7633964968133,
17.617725214094));
#202438=CARTESIAN_POINT('Ctrl Pts',(-20.1899281862006,20.7478907606142,
17.616384630862));
#202439=CARTESIAN_POINT('Ctrl Pts',(-20.1960377677347,20.7420798986383,
17.6158838479257));
#202440=CARTESIAN_POINT('Ctrl Pts',(-20.206761648039,20.7317576303522,17.6149970039737));
#202441=CARTESIAN_POINT('Ctrl Pts',(-20.2113903636002,20.7272613080624,
17.6146116014342));
#202442=CARTESIAN_POINT('Ctrl Pts',(-20.2209311219444,20.717908276504,17.6138117228439));
#202443=CARTESIAN_POINT('Ctrl Pts',(-20.2258400906605,20.71304855359,17.6133971164644));
#202444=CARTESIAN_POINT('Ctrl Pts',(-20.2379841116499,20.7009080999245,
17.6123637774134));
#202445=CARTESIAN_POINT('Ctrl Pts',(-20.2451901055315,20.6935986690433,
17.611743772359));
#202446=CARTESIAN_POINT('Ctrl Pts',(-20.2743289188332,20.6636084412211,
17.6092083273068));
#202447=CARTESIAN_POINT('Ctrl Pts',(-20.2958056583352,20.6404920002535,
17.6072732809639));
#202448=CARTESIAN_POINT('Ctrl Pts',(-20.3496120081945,20.5799172378429,
17.6022484230892));
#202449=CARTESIAN_POINT('Ctrl Pts',(-20.3811581764752,20.5417914567174,
17.5991283981105));
#202450=CARTESIAN_POINT('Ctrl Pts',(-20.456884626703,20.4434490420288,17.5911881263281));
#202451=CARTESIAN_POINT('Ctrl Pts',(-20.4992672687428,20.3819364192391,
17.5863149739154));
#202452=CARTESIAN_POINT('Ctrl Pts',(-20.6123298743042,20.1977075209771,
17.5720784258114));
#202453=CARTESIAN_POINT('Ctrl Pts',(-20.674057921606,20.0699982049781,17.5626201593295));
#202454=CARTESIAN_POINT('Ctrl Pts',(-20.722580618353,19.9371102700768,17.5536949396865));
#202455=CARTESIAN_POINT('Ctrl Pts',(-20.7225806054527,19.9371103054064,
17.3329786569753));
#202456=CARTESIAN_POINT('Ctrl Pts',(-20.7107372615498,19.9695453828509,
17.3348698511496));
#202457=CARTESIAN_POINT('Ctrl Pts',(-20.69809355522,20.0017093644426,17.3367731947366));
#202458=CARTESIAN_POINT('Ctrl Pts',(-20.6631258654366,20.084632120709,17.3417759629018));
#202459=CARTESIAN_POINT('Ctrl Pts',(-20.6395993912192,20.1348235723141,
17.3448999022645));
#202460=CARTESIAN_POINT('Ctrl Pts',(-20.5983005827594,20.2146228301491,
17.3500686680486));
#202461=CARTESIAN_POINT('Ctrl Pts',(-20.5817252546882,20.2448213735337,
17.3520736077853));
#202462=CARTESIAN_POINT('Ctrl Pts',(-20.5589828763181,20.2839602388475,
17.3547432045851));
#202463=CARTESIAN_POINT('Ctrl Pts',(-20.55347284462,20.2932775679583,17.3553841308147));
#202464=CARTESIAN_POINT('Ctrl Pts',(-20.5443331076743,20.3084655674537,
17.3564379653732));
#202465=CARTESIAN_POINT('Ctrl Pts',(-20.5407456763262,20.314361541758,17.3568493259298));
#202466=CARTESIAN_POINT('Ctrl Pts',(-20.5337470645155,20.3257381650232,
17.357647510178));
#202467=CARTESIAN_POINT('Ctrl Pts',(-20.5303395160898,20.3312209667267,
17.3580341970362));
#202468=CARTESIAN_POINT('Ctrl Pts',(-20.5224157843031,20.3438412605666,
17.3589289750136));
#202469=CARTESIAN_POINT('Ctrl Pts',(-20.5178818789106,20.350967446049,17.3594377194915));
#202470=CARTESIAN_POINT('Ctrl Pts',(-20.5055785197891,20.3700521632243,
17.3608097327707));
#202471=CARTESIAN_POINT('Ctrl Pts',(-20.4977307779454,20.381959476737,17.3616759144424));
#202472=CARTESIAN_POINT('Ctrl Pts',(-20.4097690748589,20.5125324609073,
17.3712886761429));
#202473=CARTESIAN_POINT('Ctrl Pts',(-20.3179499613997,20.6228347390983,
17.3804995450441));
#202474=CARTESIAN_POINT('Ctrl Pts',(-20.1284438847175,20.8085445979911,
17.3979634441502));
#202475=CARTESIAN_POINT('Ctrl Pts',(-20.0339203875375,20.8863599849291,
17.4061169907457));
#202476=CARTESIAN_POINT('Ctrl Pts',(-19.9081786424971,20.972793436586,17.4159185159027));
#202477=CARTESIAN_POINT('Ctrl Pts',(-19.882778923142,20.9894596629663,17.4178489467286));
#202478=CARTESIAN_POINT('Ctrl Pts',(-19.846394270088,21.0122288441255,17.4205360087966));
#202479=CARTESIAN_POINT('Ctrl Pts',(-19.8357012363898,21.0187889155282,
17.4213163850369));
#202480=CARTESIAN_POINT('Ctrl Pts',(-19.8192281999252,21.0286945109135,
17.4225036333364));
#202481=CARTESIAN_POINT('Ctrl Pts',(-19.8134898179126,21.0321082660285,
17.4229144617344));
#202482=CARTESIAN_POINT('Ctrl Pts',(-19.8039959216146,21.0376955284253,
17.4235895119217));
#202483=CARTESIAN_POINT('Ctrl Pts',(-19.8002497525258,21.0398847125606,
17.4238546919686));
#202484=CARTESIAN_POINT('Ctrl Pts',(-19.7929983829729,21.0440924104025,
17.4243656669975));
#202485=CARTESIAN_POINT('Ctrl Pts',(-19.7894940794257,21.0461124241158,
17.4246115563074));
#202486=CARTESIAN_POINT('Ctrl Pts',(-19.7829733771193,21.049846347518,17.4250671303521));
#202487=CARTESIAN_POINT('Ctrl Pts',(-19.7799585842192,21.0515628693513,
17.4252769791314));
#202488=CARTESIAN_POINT('Ctrl Pts',(-19.7730363508562,21.0554816558671,
17.4257570326747));
#202489=CARTESIAN_POINT('Ctrl Pts',(-19.7691261314201,21.0576789136537,
17.4260269140089));
#202490=CARTESIAN_POINT('Ctrl Pts',(-19.7575850076347,21.0641160076553,
17.4268197693601));
#202491=CARTESIAN_POINT('Ctrl Pts',(-19.7499347208584,21.0683211500908,
17.4273405733387));
#202492=CARTESIAN_POINT('Ctrl Pts',(-19.6951764371157,21.0979806341236,
17.4310360739689));
#202493=CARTESIAN_POINT('Ctrl Pts',(-19.6471394695405,21.1216892463029,
17.434108625441));
#202494=CARTESIAN_POINT('Ctrl Pts',(-19.4916634117191,21.1912192252019,
17.4436851942316));
#202495=CARTESIAN_POINT('Ctrl Pts',(-19.3813085562977,21.2299891372507,
17.4499509611491));
#202496=CARTESIAN_POINT('Ctrl Pts',(-19.1761931552175,21.283490717544,17.4614898217016));
#202497=CARTESIAN_POINT('Ctrl Pts',(-19.0825624455541,21.3012762190636,
17.4667180555095));
#202498=CARTESIAN_POINT('Ctrl Pts',(-18.9385360012558,21.3186864959933,
17.4749610431713));
#202499=CARTESIAN_POINT('Ctrl Pts',(-18.8888203583134,21.3229203160779,
17.477840919349));
#202500=CARTESIAN_POINT('Ctrl Pts',(-18.8267333282971,21.3260036588071,
17.4814992759886));
#202501=CARTESIAN_POINT('Ctrl Pts',(-18.8144575320636,21.3265062096081,
17.4822255760903));
#202502=CARTESIAN_POINT('Ctrl Pts',(-18.7949570560709,21.3271345507961,
17.4833843065467));
#202503=CARTESIAN_POINT('Ctrl Pts',(-18.7877347897942,21.3273302601763,
17.4838145419713));
#202504=CARTESIAN_POINT('Ctrl Pts',(-18.7741378589279,21.3276290648453,
17.484626615893));
#202505=CARTESIAN_POINT('Ctrl Pts',(-18.7677634412721,21.3277403417811,
17.4850081932904));
#202506=CARTESIAN_POINT('Ctrl Pts',(-18.7534248828736,21.3279258623002,
17.48586850014));
#202507=CARTESIAN_POINT('Ctrl Pts',(-18.7454606624291,21.3279839590941,
17.4863477305348));
#202508=CARTESIAN_POINT('Ctrl Pts',(-18.7251431478532,21.3280175150718,
17.4875738974931));
#202509=CARTESIAN_POINT('Ctrl Pts',(-18.7127901773076,21.3279297901023,
17.4883228012243));
#202510=CARTESIAN_POINT('Ctrl Pts',(-18.6394447694136,21.3267668882894,
17.4927901495022));
#202511=CARTESIAN_POINT('Ctrl Pts',(-18.5785264392339,21.323164056277,17.4965870761019));
#202512=CARTESIAN_POINT('Ctrl Pts',(-18.3707966944676,21.3018433151371,
17.5098383270292));
#202513=CARTESIAN_POINT('Ctrl Pts',(-18.2257395968538,21.2713892263614,
17.5196499713553));
#202514=CARTESIAN_POINT('Ctrl Pts',(-18.0159111296659,21.2038157892865,
17.5341823189913));
#202515=CARTESIAN_POINT('Ctrl Pts',(-17.947949759154,21.1780009850968,17.5389378098836));
#202516=CARTESIAN_POINT('Ctrl Pts',(-17.8503835164574,21.13507447377,17.5457198782743));
#202517=CARTESIAN_POINT('Ctrl Pts',(-17.8196518391715,21.1206618586582,
17.5478489603545));
#202518=CARTESIAN_POINT('Ctrl Pts',(-17.7827140675482,21.1022424156838,
17.5503876257111));
#202519=CARTESIAN_POINT('Ctrl Pts',(-17.7761670036374,21.0989350504891,
17.5508367994235));
#202520=CARTESIAN_POINT('Ctrl Pts',(-17.7659600340271,21.0937120560369,
17.5515356676651));
#202521=CARTESIAN_POINT('Ctrl Pts',(-17.7622883941272,21.0918196663564,
17.5517867789505));
#202522=CARTESIAN_POINT('Ctrl Pts',(-17.7554545829876,21.0882721180536,
17.5522535926805));
#202523=CARTESIAN_POINT('Ctrl Pts',(-17.7522910915845,21.086619726321,17.5524694583381));
#202524=CARTESIAN_POINT('Ctrl Pts',(-17.7451036055166,21.0828423086251,
17.5529593974633));
#202525=CARTESIAN_POINT('Ctrl Pts',(-17.7410822833731,21.0807123084254,
17.5532331521132));
#202526=CARTESIAN_POINT('Ctrl Pts',(-17.7288253931758,21.0741694250837,
17.5540665408118));
#202527=CARTESIAN_POINT('Ctrl Pts',(-17.7206120161803,21.0697149050539,
17.5546236018812));
#202528=CARTESIAN_POINT('Ctrl Pts',(-17.6513704198039,21.0315663617996,
17.5593102676685));
#202529=CARTESIAN_POINT('Ctrl Pts',(-17.5920046723172,20.9949275328306,
17.5632659062163));
#202530=CARTESIAN_POINT('Ctrl Pts',(-17.4067875931376,20.8675737749099,
17.5757546912446));
#202531=CARTESIAN_POINT('Ctrl Pts',(-17.2890612848439,20.7659550599222,
17.5839596662159));
#202532=CARTESIAN_POINT('Ctrl Pts',(-17.130037604616,20.5948915937186,17.5969243318276));
#202533=CARTESIAN_POINT('Ctrl Pts',(-17.079833929813,20.5344742189831,17.6013673154118));
#202534=CARTESIAN_POINT('Ctrl Pts',(-17.0216305412835,20.4559301973032,
17.6070725164429));
#202535=CARTESIAN_POINT('Ctrl Pts',(-17.0103694539777,20.440291691923,17.6082049787826));
#202536=CARTESIAN_POINT('Ctrl Pts',(-16.9943717466052,20.4174232963172,
17.6098570282562));
#202537=CARTESIAN_POINT('Ctrl Pts',(-16.9894632311524,20.4103144244406,
17.6103700374884));
#202538=CARTESIAN_POINT('Ctrl Pts',(-16.9809590426679,20.3978353580696,
17.6112697253927));
#202539=CARTESIAN_POINT('Ctrl Pts',(-16.9773441712078,20.3924783379263,
17.6116556697315));
#202540=CARTESIAN_POINT('Ctrl Pts',(-16.9703908196474,20.3820714346777,
17.6124049401289));
#202541=CARTESIAN_POINT('Ctrl Pts',(-16.9670493560623,20.3770236133315,
17.612768148682));
#202542=CARTESIAN_POINT('Ctrl Pts',(-16.9591417351451,20.3649658265094,
17.6136352578056));
#202543=CARTESIAN_POINT('Ctrl Pts',(-16.9545954158748,20.3579430290676,
17.614139894276));
#202544=CARTESIAN_POINT('Ctrl Pts',(-16.9384994771111,20.3327532279346,
17.6159486811806));
#202545=CARTESIAN_POINT('Ctrl Pts',(-16.9271857870728,20.3144377093108,
17.6172615160218));
#202546=CARTESIAN_POINT('Ctrl Pts',(-16.8182812837237,20.1319675156603,
17.6303220639662));
#202547=CARTESIAN_POINT('Ctrl Pts',(-16.7430660574381,19.9555208824072,
17.6429233810988));
#202548=CARTESIAN_POINT('Ctrl Pts',(-16.6722305095885,19.6974930882674,
17.6605786701504));
#202549=CARTESIAN_POINT('Ctrl Pts',(-16.6559617673459,19.6224944254427,
17.6656084794748));
#202550=CARTESIAN_POINT('Ctrl Pts',(-16.6382338312498,19.5121375158887,
17.6727274943662));
#202551=CARTESIAN_POINT('Ctrl Pts',(-16.6335311845082,19.4773657733027,
17.6749300831848));
#202552=CARTESIAN_POINT('Ctrl Pts',(-16.6288846328592,19.4351275686235,
17.6775440286927));
#202553=CARTESIAN_POINT('Ctrl Pts',(-16.6281132376696,19.4277598301391,
17.6779977238622));
#202554=CARTESIAN_POINT('Ctrl Pts',(-16.6269703931374,19.4162618562939,
17.6787020646977));
#202555=CARTESIAN_POINT('Ctrl Pts',(-16.6265723866486,19.4121344053361,
17.6789541628302));
#202556=CARTESIAN_POINT('Ctrl Pts',(-16.625854545772,19.4044540481614,17.6794218558287));
#202557=CARTESIAN_POINT('Ctrl Pts',(-16.6255315674642,19.4009015381619,
17.6796376197926));
#202558=CARTESIAN_POINT('Ctrl Pts',(-16.6248189947903,19.3928378102745,
17.6801261078331));
#202559=CARTESIAN_POINT('Ctrl Pts',(-16.6244348941075,19.3883261595433,
17.6803985207111));
#202560=CARTESIAN_POINT('Ctrl Pts',(-16.6234780888912,19.376644205732,17.6811016369797));
#202561=CARTESIAN_POINT('Ctrl Pts',(-16.6229274429083,19.3694720864936,
17.681531132493));
#202562=CARTESIAN_POINT('Ctrl Pts',(-16.6197242451253,19.3247664981104,
17.6841954659425));
#202563=CARTESIAN_POINT('Ctrl Pts',(-16.618036014944,19.2871681597603,17.686379984521));
#202564=CARTESIAN_POINT('Ctrl Pts',(-16.6171148458618,19.2365798023398,
17.6892673807175));
#202565=CARTESIAN_POINT('Ctrl Pts',(-16.6169978857392,19.2236151706559,
17.6900027761428));
#202566=CARTESIAN_POINT('Ctrl Pts',(-16.6170042896852,19.1848747290861,
17.692188689228));
#202567=CARTESIAN_POINT('Ctrl Pts',(-16.6174792879254,19.1591008864693,
17.6936276784161));
#202568=CARTESIAN_POINT('Ctrl Pts',(-16.6200590283671,19.0888235659277,
17.6975244091758));
#202569=CARTESIAN_POINT('Ctrl Pts',(-16.623098011573,19.0443670984207,17.6999600550654));
#202570=CARTESIAN_POINT('Ctrl Pts',(-16.6384332104871,18.8912442291542,
17.7083383509827));
#202571=CARTESIAN_POINT('Ctrl Pts',(-16.657741016693,18.7834585732879,17.7142258926028));
#202572=CARTESIAN_POINT('Ctrl Pts',(-16.7043530048111,18.6044115055277,
17.7245135041554));
#202573=CARTESIAN_POINT('Ctrl Pts',(-16.7273314285105,18.5322540763416,
17.7288036395353));
#202574=CARTESIAN_POINT('Ctrl Pts',(-16.760811013953,18.4438160500737,17.7343245780101));
#202575=CARTESIAN_POINT('Ctrl Pts',(-16.7677364774085,18.42623652406,17.7354352202146));
#202576=CARTESIAN_POINT('Ctrl Pts',(-16.7781438865704,18.4008214316912,
17.7370611386422));
#202577=CARTESIAN_POINT('Ctrl Pts',(-16.7814397140792,18.392910288821,17.7375701289746));
#202578=CARTESIAN_POINT('Ctrl Pts',(-16.7873007030189,18.3790790468757,
17.7384651578349));
#202579=CARTESIAN_POINT('Ctrl Pts',(-16.7898450758653,18.3731502195176,
17.7388504851312));
#202580=CARTESIAN_POINT('Ctrl Pts',(-16.794837010872,18.3616633272829,17.7396003275869));
#202581=CARTESIAN_POINT('Ctrl Pts',(-16.7972814688259,18.3561039760079,
17.7399647335836));
#202582=CARTESIAN_POINT('Ctrl Pts',(-16.8031802346635,18.342843753052,17.740837550642));
#202583=CARTESIAN_POINT('Ctrl Pts',(-16.8066567211035,18.3351529143772,
17.7413467199704));
#202584=CARTESIAN_POINT('Ctrl Pts',(-16.8193553198058,18.3075022473958,
17.7431880817465));
#202585=CARTESIAN_POINT('Ctrl Pts',(-16.828842015343,18.2876661293805,17.7445293717071));
#202586=CARTESIAN_POINT('Ctrl Pts',(-16.921854595549,18.1007209015869,17.7573689595346));
#202587=CARTESIAN_POINT('Ctrl Pts',(-17.0268335037852,17.9452413153183,
17.7696787408762));
#202588=CARTESIAN_POINT('Ctrl Pts',(-17.2034837459381,17.7462457880477,
17.787244444502));
#202589=CARTESIAN_POINT('Ctrl Pts',(-17.259457919604,17.6899108344471,17.7924557967283));
#202590=CARTESIAN_POINT('Ctrl Pts',(-17.3450960810183,17.6129019148492,
17.7997960844044));
#202591=CARTESIAN_POINT('Ctrl Pts',(-17.3723311964465,17.5896332902146,
17.8020457991995));
#202592=CARTESIAN_POINT('Ctrl Pts',(-17.4059330237369,17.5623694606464,
17.8047078690292));
#202593=CARTESIAN_POINT('Ctrl Pts',(-17.4117455114608,17.5577040131707,
17.8051643693612));
#202594=CARTESIAN_POINT('Ctrl Pts',(-17.4208377280944,17.5504846813245,
17.8058721037866));
#202595=CARTESIAN_POINT('Ctrl Pts',(-17.4241004777766,17.5479096481919,
17.8061248126904));
#202596=CARTESIAN_POINT('Ctrl Pts',(-17.430176662357,17.5431431651432,17.806593056121));
#202597=CARTESIAN_POINT('Ctrl Pts',(-17.4329880236853,17.5409492357654,
17.8068087633725));
#202598=CARTESIAN_POINT('Ctrl Pts',(-17.4393708521949,17.5359941049726,
17.8072963816911));
#202599=CARTESIAN_POINT('Ctrl Pts',(-17.4429456064722,17.5332372239965,
17.8075679861549));
#202600=CARTESIAN_POINT('Ctrl Pts',(-17.4535664186062,17.5251004083867,
17.8083706246931));
#202601=CARTESIAN_POINT('Ctrl Pts',(-17.4606375820238,17.5197531971771,
17.8088994079338));
#202602=CARTESIAN_POINT('Ctrl Pts',(-17.5135329503136,17.4802735547926,
17.8128151609077));
#202603=CARTESIAN_POINT('Ctrl Pts',(-17.5606929769423,17.4479612299922,
17.8160856481336));
#202604=CARTESIAN_POINT('Ctrl Pts',(-17.7373522143991,17.3371537717986,
17.8277772353816));
#202605=CARTESIAN_POINT('Ctrl Pts',(-17.8738610968989,17.2706976737131,
17.8357925855879));
#202606=CARTESIAN_POINT('Ctrl Pts',(-18.1035158456062,17.1879395951192,
17.8492379777048));
#202607=CARTESIAN_POINT('Ctrl Pts',(-18.1926940813409,17.1622763248223,
17.8544437674218));
#202608=CARTESIAN_POINT('Ctrl Pts',(-18.3038463519949,17.1380550581362,
17.8610702493794));
#202609=CARTESIAN_POINT('Ctrl Pts',(-18.3244972738103,17.1338769023156,
17.8623067836611));
#202610=CARTESIAN_POINT('Ctrl Pts',(-18.3540092729156,17.1283631522901,
17.8640829019583));
#202611=CARTESIAN_POINT('Ctrl Pts',(-18.3628222045709,17.1267744285859,
17.8646144252363));
#202612=CARTESIAN_POINT('Ctrl Pts',(-18.3780651986401,17.124126289835,17.8655358187572));
#202613=CARTESIAN_POINT('Ctrl Pts',(-18.3844906078812,17.123040553949,17.865924846753));
#202614=CARTESIAN_POINT('Ctrl Pts',(-18.3968182773979,17.1210159801144,
17.8666724770175));
#202615=CARTESIAN_POINT('Ctrl Pts',(-18.4027197092853,17.1200724342341,
17.8670309256468));
#202616=CARTESIAN_POINT('Ctrl Pts',(-18.4181096284813,17.1176786181755,
17.867967160809));
#202617=CARTESIAN_POINT('Ctrl Pts',(-18.4276040451626,17.1162678814382,
17.8685461945864));
#202618=CARTESIAN_POINT('Ctrl Pts',(-18.4601866623367,17.1116528193219,
17.8705384378405));
#202619=CARTESIAN_POINT('Ctrl Pts',(-18.483317371144,17.1087653603039,17.8719615972887));
#202620=CARTESIAN_POINT('Ctrl Pts',(-18.6762834447713,17.0879068901408,
17.8839119107713));
#202621=CARTESIAN_POINT('Ctrl Pts',(-18.8476432299002,17.0901701865104,
17.8951009097751));
#202622=CARTESIAN_POINT('Ctrl Pts',(-19.1063740477653,17.1250493423621,
17.9123529957993));
#202623=CARTESIAN_POINT('Ctrl Pts',(-19.1950575677666,17.1428412794891,
17.9183161543863));
#202624=CARTESIAN_POINT('Ctrl Pts',(-19.3196739190989,17.1762593939394,
17.926559300344));
#202625=CARTESIAN_POINT('Ctrl Pts',(-19.3567321142378,17.1872933950379,
17.9289921969329));
#202626=CARTESIAN_POINT('Ctrl Pts',(-19.4007094570309,17.2017101891573,
17.9318403551817));
#202627=CARTESIAN_POINT('Ctrl Pts',(-19.4079362977276,17.2041225959948,
17.9323071167012));
#202628=CARTESIAN_POINT('Ctrl Pts',(-19.419119572097,17.2079229299966,17.9330272534485));
#202629=CARTESIAN_POINT('Ctrl Pts',(-19.423085085747,17.2092836560222,17.933282186451));
#202630=CARTESIAN_POINT('Ctrl Pts',(-19.4304131490909,17.211822564126,17.9337524721009));
#202631=CARTESIAN_POINT('Ctrl Pts',(-19.43377673889,17.2129974448585,17.9339680105886));
#202632=CARTESIAN_POINT('Ctrl Pts',(-19.4413507316474,17.2156644654282,
17.9344526336642));
#202633=CARTESIAN_POINT('Ctrl Pts',(-19.4455593750435,17.2171614384018,
17.9347214276589));
#202634=CARTESIAN_POINT('Ctrl Pts',(-19.4578987888647,17.2215944927505,
17.9355081380936));
#202635=CARTESIAN_POINT('Ctrl Pts',(-19.4660164632558,17.2245671085841,
17.9360239344966));
#202636=CARTESIAN_POINT('Ctrl Pts',(-19.5224620839178,17.2456299683968,
17.9395997359455));
#202637=CARTESIAN_POINT('Ctrl Pts',(-19.570136866398,17.2654337864405,17.9425649448127));
#202638=CARTESIAN_POINT('Ctrl Pts',(-19.6369258537576,17.2960868296322,
17.9467038075734));
#202639=CARTESIAN_POINT('Ctrl Pts',(-19.6566654900655,17.3055194866697,
17.9479250922272));
#202640=CARTESIAN_POINT('Ctrl Pts',(-19.7995548873995,17.3765408966788,
17.9567753038505));
#202641=CARTESIAN_POINT('Ctrl Pts',(-19.916583287637,17.4497087583583,17.9640986673369));
#202642=CARTESIAN_POINT('Ctrl Pts',(-20.0975674204316,17.5890858973673,
17.9766928902694));
#202643=CARTESIAN_POINT('Ctrl Pts',(-20.1658131855151,17.6490045663342,
17.9817933921475));
#202644=CARTESIAN_POINT('Ctrl Pts',(-20.2447378821601,17.7278297923862,
17.9882924957569));
#202645=CARTESIAN_POINT('Ctrl Pts',(-20.2592564965341,17.74276453268,17.9895151166081));
#202646=CARTESIAN_POINT('Ctrl Pts',(-20.2796703579813,17.7643930734421,
17.9912747006375));
#202647=CARTESIAN_POINT('Ctrl Pts',(-20.2857476201939,17.7709139695741,
17.9918038099723));
#202648=CARTESIAN_POINT('Ctrl Pts',(-20.2961911316462,17.7822627122393,
17.9927223534401));
#202649=CARTESIAN_POINT('Ctrl Pts',(-20.3005766617647,17.7870727088133,
17.9931109595467));
#202650=CARTESIAN_POINT('Ctrl Pts',(-20.3089521410906,17.7963443603903,
17.993858720674));
#202651=CARTESIAN_POINT('Ctrl Pts',(-20.3129454934828,17.800802867372,17.9942177265764));
#202652=CARTESIAN_POINT('Ctrl Pts',(-20.3233262651086,17.8124921857426,
17.9951575132199));
#202653=CARTESIAN_POINT('Ctrl Pts',(-20.3296832024114,17.8197497722463,
17.9957395598317));
#202654=CARTESIAN_POINT('Ctrl Pts',(-20.3514219108505,17.8449134054578,
17.997752883754));
#202655=CARTESIAN_POINT('Ctrl Pts',(-20.366553229559,17.8630326030041,17.9991943958255));
#202656=CARTESIAN_POINT('Ctrl Pts',(-20.4850678414537,18.0098725749781,
18.0108162033018));
#202657=CARTESIAN_POINT('Ctrl Pts',(-20.5733548934424,18.1500100955293,
18.0216100250107));
#202658=CARTESIAN_POINT('Ctrl Pts',(-20.6994383638687,18.4141136283923,
18.0409499476056));
#202659=CARTESIAN_POINT('Ctrl Pts',(-20.7438992365239,18.534030521824,18.0493910847454));
#202660=CARTESIAN_POINT('Ctrl Pts',(-20.7804090212664,18.6687441839928,
18.0580465963771));
#202661=CARTESIAN_POINT('Ctrl Pts',(-20.7834316336782,18.6802823290836,
18.0587813705075));
#202662=CARTESIAN_POINT('Ctrl Pts',(-20.787589128825,18.6967180262668,18.0598181150712));
#202663=CARTESIAN_POINT('Ctrl Pts',(-20.7888042685242,18.701594780371,18.0601244989699));
#202664=CARTESIAN_POINT('Ctrl Pts',(-20.7908681038565,18.7100051802587,
18.060650701977));
#202665=CARTESIAN_POINT('Ctrl Pts',(-20.7917250850009,18.7135367537126,
18.0608709949494));
#202666=CARTESIAN_POINT('Ctrl Pts',(-20.7933688049623,18.7203873630446,
18.0612970197116));
#202667=CARTESIAN_POINT('Ctrl Pts',(-20.794156616175,18.7237060932013,18.0615028153574));
#202668=CARTESIAN_POINT('Ctrl Pts',(-20.7962599601198,18.7326629064712,
18.0620566780443));
#202669=CARTESIAN_POINT('Ctrl Pts',(-20.7975604026104,18.7383045539363,
18.0624038835368));
#202670=CARTESIAN_POINT('Ctrl Pts',(-20.802298076856,18.7592499787697,18.063687031871));
#202671=CARTESIAN_POINT('Ctrl Pts',(-20.8055884394109,18.7745869082983,
18.0646149284832));
#202672=CARTESIAN_POINT('Ctrl Pts',(-20.8354454531704,18.9217095450431,
18.0734168415235));
#202673=CARTESIAN_POINT('Ctrl Pts',(-20.8495760153237,19.0557259553302,
18.0806879720517));
#202674=CARTESIAN_POINT('Ctrl Pts',(-20.8509595374546,19.1964793462705,
18.0883318990536));
#202675=CARTESIAN_POINT('Ctrl Pts',(-20.8509933270319,19.2027667816616,
18.0886733340331));
#202676=CARTESIAN_POINT('Ctrl Pts',(-20.8511331455446,19.3548927652846,
18.0969355644505));
#202677=CARTESIAN_POINT('Ctrl Pts',(-20.8361978951726,19.5003359712167,
18.1048962803306));
#202678=CARTESIAN_POINT('Ctrl Pts',(-20.8015323056837,19.6666057069565,
18.1147555389692));
#202679=CARTESIAN_POINT('Ctrl Pts',(-20.7962279558318,19.690042987735,18.1161623214917));
#202680=CARTESIAN_POINT('Ctrl Pts',(-20.7882195563418,19.7228256285329,
18.1181560508981));
#202681=CARTESIAN_POINT('Ctrl Pts',(-20.7858481762291,19.7322509152032,
18.1187323030259));
#202682=CARTESIAN_POINT('Ctrl Pts',(-20.7819083815182,19.7474664419076,
18.1196676110311));
#202683=CARTESIAN_POINT('Ctrl Pts',(-20.7803800924553,19.7532669992248,
18.1200253656573));
#202684=CARTESIAN_POINT('Ctrl Pts',(-20.7771446742239,19.7653384144605,
18.1207723986571));
#202685=CARTESIAN_POINT('Ctrl Pts',(-20.7754332818565,19.7716080554388,
18.1211618120893));
#202686=CARTESIAN_POINT('Ctrl Pts',(-20.7713216373953,19.7864024486274,
18.1220841100033));
#202687=CARTESIAN_POINT('Ctrl Pts',(-20.7688967216706,19.7949201662001,
18.1226177924416));
#202688=CARTESIAN_POINT('Ctrl Pts',(-20.7606830621833,19.8230987014574,
18.1243923673513));
#202689=CARTESIAN_POINT('Ctrl Pts',(-20.7546623942917,19.8426901905225,
18.1256408005816));
#202690=CARTESIAN_POINT('Ctrl Pts',(-20.7402319533099,19.8873285460168,
18.1285198080292));
#202691=CARTESIAN_POINT('Ctrl Pts',(-20.7316376301585,19.9123060540526,
18.1301559494639));
#202692=CARTESIAN_POINT('Ctrl Pts',(-20.7225805905512,19.9371103462167,
18.1318063719887));
#202693=CARTESIAN_POINT('Origin',(-18.734,19.211,0.));
#202694=CARTESIAN_POINT('',(-20.7202231500468,19.93627084876,19.1554367712949));
#202695=CARTESIAN_POINT('',(-20.7225805923249,19.9371103413593,18.9348455557956));
#202696=CARTESIAN_POINT('',(-20.7225806064498,19.9371103026755,0.));
#202697=CARTESIAN_POINT('',(-20.8499620916056,19.2091158126,19.1109437209775));
#202698=CARTESIAN_POINT('Ctrl Pts',(-20.8499620916056,19.2091158126,19.1109437209775));
#202699=CARTESIAN_POINT('Ctrl Pts',(-20.8478499414866,19.4559462748795,
19.12577473775));
#202700=CARTESIAN_POINT('Ctrl Pts',(-20.8034780786863,19.7034419500621,
19.1406057545224));
#202701=CARTESIAN_POINT('Ctrl Pts',(-20.7202231500468,19.93627084876,19.1554367712949));
#202702=CARTESIAN_POINT('Ctrl Pts',(-20.8509991255302,19.2090758107338,
19.1115402065938));
#202703=CARTESIAN_POINT('Ctrl Pts',(-20.8509516894146,19.1568864461007,
19.108121049185));
#202704=CARTESIAN_POINT('Ctrl Pts',(-20.8489743712533,19.1047170798901,
19.1046744518397));
#202705=CARTESIAN_POINT('Ctrl Pts',(-20.8355939732812,18.9263061605855,
19.0928511306297));
#202706=CARTESIAN_POINT('Ctrl Pts',(-20.8147881617888,18.8010303123376,
19.0844726261103));
#202707=CARTESIAN_POINT('Ctrl Pts',(-20.7798982971389,18.6668205583257,
19.0758731777046));
#202708=CARTESIAN_POINT('Ctrl Pts',(-20.7768015033896,18.6553084131162,
19.0751387839972));
#202709=CARTESIAN_POINT('Ctrl Pts',(-20.7722613418263,18.6389816869146,
19.0741024790361));
#202710=CARTESIAN_POINT('Ctrl Pts',(-20.7708978864628,18.6341453827811,
19.0737961593069));
#202711=CARTESIAN_POINT('Ctrl Pts',(-20.7685187432036,18.6258199522268,
19.0732700314745));
#202712=CARTESIAN_POINT('Ctrl Pts',(-20.7675112714562,18.6223285174239,
19.0730497498653));
#202713=CARTESIAN_POINT('Ctrl Pts',(-20.7655406248523,18.6155645913163,
19.0726237195193));
#202714=CARTESIAN_POINT('Ctrl Pts',(-20.764578530616,18.6122918342616,19.0724179070573));
#202715=CARTESIAN_POINT('Ctrl Pts',(-20.7619618414276,18.6034695030517,
19.0718639407828));
#202716=CARTESIAN_POINT('Ctrl Pts',(-20.760292365231,18.5979243216301,19.0715166490958));
#202717=CARTESIAN_POINT('Ctrl Pts',(-20.7540140035938,18.5773764977283,
19.0702328458126));
#202718=CARTESIAN_POINT('Ctrl Pts',(-20.7492609525142,18.5624179749817,
19.069304391038));
#202719=CARTESIAN_POINT('Ctrl Pts',(-20.6977077257283,18.4062134970419,
19.0596600658168));
#202720=CARTESIAN_POINT('Ctrl Pts',(-20.6362994852711,18.2702031321059,
19.0516823747842));
#202721=CARTESIAN_POINT('Ctrl Pts',(-20.5205652768002,18.0724387348816,
19.0392298958366));
#202722=CARTESIAN_POINT('Ctrl Pts',(-20.4760980019424,18.0054997670339,
19.0348482182288));
#202723=CARTESIAN_POINT('Ctrl Pts',(-20.3988169588823,17.9024011865837,
19.0276435918523));
#202724=CARTESIAN_POINT('Ctrl Pts',(-20.3683694435708,17.8645667791617,
19.0248921510687));
#202725=CARTESIAN_POINT('Ctrl Pts',(-20.3163399544824,17.8042820051318,
19.0202985329374));
#202726=CARTESIAN_POINT('Ctrl Pts',(-20.2955152301747,17.7812009626752,
19.0184859975746));
#202727=CARTESIAN_POINT('Ctrl Pts',(-20.26717632535,17.7511493625238,19.0160488582923));
#202728=CARTESIAN_POINT('Ctrl Pts',(-20.2601082998709,17.7437621256712,
19.0154433564929));
#202729=CARTESIAN_POINT('Ctrl Pts',(-20.2481822913166,17.7314769101663,
19.0144254279768));
#202730=CARTESIAN_POINT('Ctrl Pts',(-20.2433533296475,17.7265509071584,
19.0140142692992));
#202731=CARTESIAN_POINT('Ctrl Pts',(-20.2339579094634,17.7170599206848,
19.013216201102));
#202732=CARTESIAN_POINT('Ctrl Pts',(-20.2293944668913,17.7124920495025,
19.0128294269554));
#202733=CARTESIAN_POINT('Ctrl Pts',(-20.2188074257031,17.7019912553693,
19.0119340455725));
#202734=CARTESIAN_POINT('Ctrl Pts',(-20.2127690695207,17.6960734279891,
19.0114247821942));
#202735=CARTESIAN_POINT('Ctrl Pts',(-20.1964298236759,17.6802510929699,
19.0100504613606));
#202736=CARTESIAN_POINT('Ctrl Pts',(-20.1860639670904,17.670414583572,19.0091824757563));
#202737=CARTESIAN_POINT('Ctrl Pts',(-20.0900233636271,17.5811088655016,
19.0011746983341));
#202738=CARTESIAN_POINT('Ctrl Pts',(-19.9980197569223,17.5087688997371,
18.9937330845983));
#202739=CARTESIAN_POINT('Ctrl Pts',(-19.7647250564385,17.3547186341645,
18.9754718456826));
#202740=CARTESIAN_POINT('Ctrl Pts',(-19.619033802088,17.2810026174587,18.96451211118));
#202741=CARTESIAN_POINT('Ctrl Pts',(-19.4358588681189,17.2134669361007,
18.952107146499));
#202742=CARTESIAN_POINT('Ctrl Pts',(-19.4051238166674,17.2029319476545,
18.95007122557));
#202743=CARTESIAN_POINT('Ctrl Pts',(-19.3672574607857,17.1909192152583,
18.9476283632737));
#202744=CARTESIAN_POINT('Ctrl Pts',(-19.3603470229541,17.1887658892093,
18.9471851906261));
#202745=CARTESIAN_POINT('Ctrl Pts',(-19.3494960884831,17.1854456434043,
18.9464935907858));
#202746=CARTESIAN_POINT('Ctrl Pts',(-19.3455630824792,17.1842547068579,
18.9462437936542));
#202747=CARTESIAN_POINT('Ctrl Pts',(-19.3382049520362,17.1820499920733,
18.9457781304773));
#202748=CARTESIAN_POINT('Ctrl Pts',(-19.3347807673545,17.1810334415223,
18.945562109106));
#202749=CARTESIAN_POINT('Ctrl Pts',(-19.3269582586138,17.1787326708496,
18.9450701450696));
#202750=CARTESIAN_POINT('Ctrl Pts',(-19.3225583364721,17.1774540627109,
18.9447945317634));
#202751=CARTESIAN_POINT('Ctrl Pts',(-19.3090209435828,17.1735677418406,
18.9439498269588));
#202752=CARTESIAN_POINT('Ctrl Pts',(-19.2998698941502,17.1710072150481,
18.9433834114928));
#202753=CARTESIAN_POINT('Ctrl Pts',(-19.2174761923205,17.1485499798146,
18.9383221687416));
#202754=CARTESIAN_POINT('Ctrl Pts',(-19.1432216932006,17.1325415507712,
18.9340337611397));
#202755=CARTESIAN_POINT('Ctrl Pts',(-18.9181952179629,17.0965600397241,
18.9214210653693));
#202756=CARTESIAN_POINT('Ctrl Pts',(-18.7659829277571,17.0887926840675,
18.9133657723101));
#202757=CARTESIAN_POINT('Ctrl Pts',(-18.559227941065,17.1005070466343,18.901850981901));
#202758=CARTESIAN_POINT('Ctrl Pts',(-18.5043552591716,17.1057711700339,
18.8987436322711));
#202759=CARTESIAN_POINT('Ctrl Pts',(-18.4157574817194,17.1177757841177,
18.893599872603));
#202760=CARTESIAN_POINT('Ctrl Pts',(-18.3818804108329,17.12320750151,18.8916028451718));
#202761=CARTESIAN_POINT('Ctrl Pts',(-18.3375239044313,17.1314297235214,
18.8889422945815));
#202762=CARTESIAN_POINT('Ctrl Pts',(-18.3269115927588,17.1334810828053,
18.8883022975686));
#202763=CARTESIAN_POINT('Ctrl Pts',(-18.309553058374,17.1369745956055,18.8872496021747));
#202764=CARTESIAN_POINT('Ctrl Pts',(-18.3027972696982,17.1383686319131,
18.8868384450124));
#202765=CARTESIAN_POINT('Ctrl Pts',(-18.2897313051546,17.1411314008716,
18.8860403777034));
#202766=CARTESIAN_POINT('Ctrl Pts',(-18.2834203337178,17.1424960348654,
18.8856536029188));
#202767=CARTESIAN_POINT('Ctrl Pts',(-18.2688601920183,17.1457141982544,
18.8847582170681));
#202768=CARTESIAN_POINT('Ctrl Pts',(-18.2606157268999,17.1475883080191,
18.8842489498393));
#202769=CARTESIAN_POINT('Ctrl Pts',(-18.2384672506628,17.1527627672891,
18.8828746118452));
#202770=CARTESIAN_POINT('Ctrl Pts',(-18.2245852508197,17.1561545534074,
18.8820066128172));
#202771=CARTESIAN_POINT('Ctrl Pts',(-18.0974921218371,17.1885742154504,
18.8739978114357));
#202772=CARTESIAN_POINT('Ctrl Pts',(-17.9868506330444,17.2267852069755,
18.8665550976252));
#202773=CARTESIAN_POINT('Ctrl Pts',(-17.7309819747738,17.3395978556687,
18.8482893605931));
#202774=CARTESIAN_POINT('Ctrl Pts',(-17.5900993418143,17.422234360456,18.8373260994925));
#202775=CARTESIAN_POINT('Ctrl Pts',(-17.4341820375042,17.5397090069427,
18.8249224243594));
#202776=CARTESIAN_POINT('Ctrl Pts',(-17.4087356316912,17.5598140807818,
18.8228903476481));
#202777=CARTESIAN_POINT('Ctrl Pts',(-17.3781881188452,17.5851108672491,
18.8204514483935));
#202778=CARTESIAN_POINT('Ctrl Pts',(-17.3726402090257,17.589753303141,18.8200085301963));
#202779=CARTESIAN_POINT('Ctrl Pts',(-17.3639788635493,17.5970768405167,
18.8193172386712));
#202780=CARTESIAN_POINT('Ctrl Pts',(-17.3608493116709,17.5997386720824,
18.8190674973748));
#202781=CARTESIAN_POINT('Ctrl Pts',(-17.355013283545,17.6047318419703,18.8186018825525));
#202782=CARTESIAN_POINT('Ctrl Pts',(-17.3523049887731,17.6070608939741,
18.8183858540368));
#202783=CARTESIAN_POINT('Ctrl Pts',(-17.3461351185857,17.6123940207103,
18.8178938015523));
#202784=CARTESIAN_POINT('Ctrl Pts',(-17.3426774022816,17.615402483059,18.8176181074007));
#202785=CARTESIAN_POINT('Ctrl Pts',(-17.3320758871606,17.6246872294373,
18.8167729084355));
#202786=CARTESIAN_POINT('Ctrl Pts',(-17.3249644703827,17.631000535406,18.816206084201));
#202787=CARTESIAN_POINT('Ctrl Pts',(-17.2286610701478,17.7176631811832,
18.8085279725265));
#202788=CARTESIAN_POINT('Ctrl Pts',(-17.1464047277001,17.8054218983844,
18.8019382913532));
#202789=CARTESIAN_POINT('Ctrl Pts',(-17.0046327502323,17.9851064714334,
18.7894810467888));
#202790=CARTESIAN_POINT('Ctrl Pts',(-16.9439268368985,18.0755867921844,
18.7836199419601));
#202791=CARTESIAN_POINT('Ctrl Pts',(-16.8536586056344,18.235497260102,18.7734039861693));
#202792=CARTESIAN_POINT('Ctrl Pts',(-16.8203558046817,18.3025653263309,
18.7691597391762));
#202793=CARTESIAN_POINT('Ctrl Pts',(-16.7832259174287,18.3884903257147,
18.7636941062077));
#202794=CARTESIAN_POINT('Ctrl Pts',(-16.7760064074826,18.4058275069566,
18.7625900826683));
#202795=CARTESIAN_POINT('Ctrl Pts',(-16.7658374710658,18.4311933896602,
18.7609720988818));
#202796=CARTESIAN_POINT('Ctrl Pts',(-16.7627044009515,18.4391478459372,
18.7604643372393));
#202797=CARTESIAN_POINT('Ctrl Pts',(-16.7572928130651,18.4531350513834,
18.7595707284595));
#202798=CARTESIAN_POINT('Ctrl Pts',(-16.7549935041877,18.4591596769698,
18.7591855855115));
#202799=CARTESIAN_POINT('Ctrl Pts',(-16.7505801062103,18.4708841429516,
18.758435550657));
#202800=CARTESIAN_POINT('Ctrl Pts',(-16.7484629705489,18.4765827749738,
18.7580707653219));
#202801=CARTESIAN_POINT('Ctrl Pts',(-16.7434571483718,18.4902366642788,
18.7571961476977));
#202802=CARTESIAN_POINT('Ctrl Pts',(-16.7405915820036,18.4982002342207,
18.7566855500572));
#202803=CARTESIAN_POINT('Ctrl Pts',(-16.7304040956047,18.5270537659047,
18.7548336947767));
#202804=CARTESIAN_POINT('Ctrl Pts',(-16.7233623787762,18.5480405012563,
18.7534832039145));
#202805=CARTESIAN_POINT('Ctrl Pts',(-16.6604503530236,18.745769212172,18.7407222535653));
#202806=CARTESIAN_POINT('Ctrl Pts',(-16.6277020998735,18.928990290587,18.728514762743));
#202807=CARTESIAN_POINT('Ctrl Pts',(-16.6155433094807,19.1943019699739,
18.7109795572108));
#202808=CARTESIAN_POINT('Ctrl Pts',(-16.6164340970995,19.2746705786126,
18.7057030263833));
#202809=CARTESIAN_POINT('Ctrl Pts',(-16.6243396653045,19.3907872072471,
18.6982836184296));
#202810=CARTESIAN_POINT('Ctrl Pts',(-16.6277094524878,19.4267096579234,
18.6960172700313));
#202811=CARTESIAN_POINT('Ctrl Pts',(-16.6328832983173,19.4699466914154,
18.693338239438));
#202812=CARTESIAN_POINT('Ctrl Pts',(-16.6338099568734,19.477357972771,18.6928807658437));
#202813=CARTESIAN_POINT('Ctrl Pts',(-16.635313775009,19.4888892466954,18.6921718543056));
#202814=CARTESIAN_POINT('Ctrl Pts',(-16.6358638777318,19.493012619428,18.6919189337654));
#202815=CARTESIAN_POINT('Ctrl Pts',(-16.6369080897043,19.5006674552641,
18.6914504985302));
#202816=CARTESIAN_POINT('Ctrl Pts',(-16.6373989625544,19.5041992580581,
18.6912348098564));
#202817=CARTESIAN_POINT('Ctrl Pts',(-16.6385308602937,19.5121949886956,
18.6907474880104));
#202818=CARTESIAN_POINT('Ctrl Pts',(-16.6391772248875,19.5166581070596,
18.69047615987));
#202819=CARTESIAN_POINT('Ctrl Pts',(-16.6408827680919,19.5281752408796,
18.6897776948434));
#202820=CARTESIAN_POINT('Ctrl Pts',(-16.6419633554103,19.535226095327,18.6893517394058));
#202821=CARTESIAN_POINT('Ctrl Pts',(-16.6488138792592,19.5784652562542,
18.6867489664919));
#202822=CARTESIAN_POINT('Ctrl Pts',(-16.6554873799883,19.6145065355942,
18.6846198421916));
#202823=CARTESIAN_POINT('Ctrl Pts',(-16.6985016282384,19.8172531114208,
18.6727801149832));
#202824=CARTESIAN_POINT('Ctrl Pts',(-16.7539571675207,19.979270088939,18.6638037167283));
#202825=CARTESIAN_POINT('Ctrl Pts',(-16.8697799711943,20.2187004902832,
18.649172630837));
#202826=CARTESIAN_POINT('Ctrl Pts',(-16.9170369077137,20.3016047160456,
18.643827422453));
#202827=CARTESIAN_POINT('Ctrl Pts',(-16.9815335280367,20.398858380119,18.6370321384681));
#202828=CARTESIAN_POINT('Ctrl Pts',(-16.9936210628571,20.4164988064763,
18.635777390431));
#202829=CARTESIAN_POINT('Ctrl Pts',(-17.0111774721167,20.4413059336624,
18.6339796512418));
#202830=CARTESIAN_POINT('Ctrl Pts',(-17.0164283373035,20.4486258451847,
18.633444995718));
#202831=CARTESIAN_POINT('Ctrl Pts',(-17.0255634541739,20.4611904494717,
18.6325198962453));
#202832=CARTESIAN_POINT('Ctrl Pts',(-17.029425561523,20.4664511433283,18.6321303130682));
#202833=CARTESIAN_POINT('Ctrl Pts',(-17.0368641792246,20.4764859099862,
18.6313828196084));
#202834=CARTESIAN_POINT('Ctrl Pts',(-17.0404366688373,20.4812628959164,
18.6310250687564));
#202835=CARTESIAN_POINT('Ctrl Pts',(-17.0497729168165,20.493637547185,18.6300933050721));
#202836=CARTESIAN_POINT('Ctrl Pts',(-17.0555678617548,20.5012114159425,
18.629518068344));
#202837=CARTESIAN_POINT('Ctrl Pts',(-17.0754716082051,20.5268641547522,
18.6275526135447));
#202838=CARTESIAN_POINT('Ctrl Pts',(-17.0898225243021,20.544752324703,18.6261528028665));
#202839=CARTESIAN_POINT('Ctrl Pts',(-17.2170159590825,20.6981237804615,
18.6138892561262));
#202840=CARTESIAN_POINT('Ctrl Pts',(-17.3460659156701,20.819226643004,18.6023142772999));
#202841=CARTESIAN_POINT('Ctrl Pts',(-17.5584852768959,20.9737604683381,
18.5849591995691));
#202842=CARTESIAN_POINT('Ctrl Pts',(-17.631430743594,21.0202822526329,18.5792643130506));
#202843=CARTESIAN_POINT('Ctrl Pts',(-17.7399657190424,21.080493057856,18.5713409505952));
#202844=CARTESIAN_POINT('Ctrl Pts',(-17.7733956414394,21.0978884749886,
18.5689712915508));
#202845=CARTESIAN_POINT('Ctrl Pts',(-17.8140744686911,21.1176943174974,
18.5661872042153));
#202846=CARTESIAN_POINT('Ctrl Pts',(-17.8208924054788,21.1209687767929,
18.5657238742943));
#202847=CARTESIAN_POINT('Ctrl Pts',(-17.8315058502969,21.1259962886751,
18.5650078831804));
#202848=CARTESIAN_POINT('Ctrl Pts',(-17.8352891693654,21.1277747179794,
18.5647536921738));
#202849=CARTESIAN_POINT('Ctrl Pts',(-17.8423075547456,21.1310485109308,
18.5642840942205));
#202850=CARTESIAN_POINT('Ctrl Pts',(-17.8455411008406,21.1325468992593,
18.5640685057935));
#202851=CARTESIAN_POINT('Ctrl Pts',(-17.8528501348538,21.1359114281825,
18.5635829123951));
#202852=CARTESIAN_POINT('Ctrl Pts',(-17.8569277632702,21.1377727898229,
18.5633132032368));
#202853=CARTESIAN_POINT('Ctrl Pts',(-17.8689518254206,21.1432154709269,
18.5625213223534));
#202854=CARTESIAN_POINT('Ctrl Pts',(-17.8769146113193,21.1467607323357,
18.5620013126987));
#202855=CARTESIAN_POINT('Ctrl Pts',(-17.9337070100982,21.1716272020756,
18.5583221566122));
#202856=CARTESIAN_POINT('Ctrl Pts',(-17.9833086758754,21.1911493497732,
18.5552641461112));
#202857=CARTESIAN_POINT('Ctrl Pts',(-18.0356440139679,21.2094975895958,
18.5521451003604));
#202858=CARTESIAN_POINT('Ctrl Pts',(-18.0376907282989,21.2102116188758,
18.5520232905384));
#202859=CARTESIAN_POINT('Ctrl Pts',(-18.1790205433749,21.2592734416253,
18.5436234960636));
#202860=CARTESIAN_POINT('Ctrl Pts',(-18.322979181674,21.2929446935847,18.5358056356231));
#202861=CARTESIAN_POINT('Ctrl Pts',(-18.5662414571187,21.3236044769383,
18.522332945513));
#202862=CARTESIAN_POINT('Ctrl Pts',(-18.6639257798467,21.3290951254383,
18.5168602791409));
#202863=CARTESIAN_POINT('Ctrl Pts',(-18.783299637179,21.3275368086815,18.5099105333103));
#202864=CARTESIAN_POINT('Ctrl Pts',(-18.8049598843882,21.3269213502096,
18.5086393390396));
#202865=CARTESIAN_POINT('Ctrl Pts',(-18.8356539658716,21.3255773782255,
18.5068220999333));
#202866=CARTESIAN_POINT('Ctrl Pts',(-18.8446988915386,21.3251231678433,
18.5062846428918));
#202867=CARTESIAN_POINT('Ctrl Pts',(-18.8602650000054,21.3242413149596,
18.505356221637));
#202868=CARTESIAN_POINT('Ctrl Pts',(-18.8667876775168,21.323841484045,18.5049661348351));
#202869=CARTESIAN_POINT('Ctrl Pts',(-18.8792508224765,21.3230195702709,
18.5042187334738));
#202870=CARTESIAN_POINT('Ctrl Pts',(-18.8851915736479,21.3226026078713,
18.5038615834564));
#202871=CARTESIAN_POINT('Ctrl Pts',(-18.9005868951636,21.3214567577393,
18.5029336937404));
#202872=CARTESIAN_POINT('Ctrl Pts',(-18.9100383920755,21.3206894083886,
18.5023617502846));
#202873=CARTESIAN_POINT('Ctrl Pts',(-18.9420029207091,21.3178779737555,
18.5004195299524));
#202874=CARTESIAN_POINT('Ctrl Pts',(-18.9644876566442,21.3155368586171,
18.4990399655902));
#202875=CARTESIAN_POINT('Ctrl Pts',(-19.1659636333705,21.2912917226362,
18.4865540242466));
#202876=CARTESIAN_POINT('Ctrl Pts',(-19.3414790078144,21.2469641746786,
18.4746991957193));
#202877=CARTESIAN_POINT('Ctrl Pts',(-19.5870772016413,21.1503168477156,
18.4572661070518));
#202878=CARTESIAN_POINT('Ctrl Pts',(-19.6630607017603,21.1150847106651,
18.4517594970013));
#202879=CARTESIAN_POINT('Ctrl Pts',(-19.7693186806952,21.0579354803178,
18.444062116749));
#202880=CARTESIAN_POINT('Ctrl Pts',(-19.8014123158424,21.0395750659402,
18.4417382248148));
#202881=CARTESIAN_POINT('Ctrl Pts',(-19.8394398199671,21.0164773291489,
18.4390006181416));
#202882=CARTESIAN_POINT('Ctrl Pts',(-19.8458481296641,21.0125380434795,
18.438539843267));
#202883=CARTESIAN_POINT('Ctrl Pts',(-19.8557774389215,21.0063611833208,
18.4378269401707));
#202884=CARTESIAN_POINT('Ctrl Pts',(-19.8593129767356,21.0041472628124,
18.4375733028131));
#202885=CARTESIAN_POINT('Ctrl Pts',(-19.8658575976277,21.0000221031603,
18.4371042138961));
#202886=CARTESIAN_POINT('Ctrl Pts',(-19.8688683701277,20.9981137316007,
18.4368885841197));
#202887=CARTESIAN_POINT('Ctrl Pts',(-19.8756640900429,20.9937821802581,
18.4364022481211));
#202888=CARTESIAN_POINT('Ctrl Pts',(-19.8794461398497,20.9913545540983,
18.436131841685));
#202889=CARTESIAN_POINT('Ctrl Pts',(-19.8905864055577,20.9841536348853,
18.4353360109431));
#202890=CARTESIAN_POINT('Ctrl Pts',(-19.8979228248307,20.9793465696196,
18.4348127810934));
#202891=CARTESIAN_POINT('Ctrl Pts',(-19.9507592810769,20.9442550936977,
18.4310491635101));
#202892=CARTESIAN_POINT('Ctrl Pts',(-19.9951053824365,20.9122614940637,
18.4279152610807));
#202893=CARTESIAN_POINT('Ctrl Pts',(-20.1707479744334,20.7748967603769,
18.4153889348266));
#202894=CARTESIAN_POINT('Ctrl Pts',(-20.2904962805355,20.6557645756205,
18.4065304697253));
#202895=CARTESIAN_POINT('Ctrl Pts',(-20.4314204825302,20.4774620379215,
18.3939311570114));
#202896=CARTESIAN_POINT('Ctrl Pts',(-20.4660158367833,20.429721775069,18.3906172273238));
#202897=CARTESIAN_POINT('Ctrl Pts',(-20.5184688932347,20.3505861641391,
18.3851630618666));
#202898=CARTESIAN_POINT('Ctrl Pts',(-20.5375946958178,20.3200679886129,
18.3830687427483));
#202899=CARTESIAN_POINT('Ctrl Pts',(-20.5615339482237,20.2796110957751,
18.3802971236516));
#202900=CARTESIAN_POINT('Ctrl Pts',(-20.5670618584833,20.2701006665981,
18.3796459307387));
#202901=CARTESIAN_POINT('Ctrl Pts',(-20.5759561099417,20.2545204149895,
18.3785795032806));
#202902=CARTESIAN_POINT('Ctrl Pts',(-20.5793672076699,20.2484762814373,
18.3781658896052));
#202903=CARTESIAN_POINT('Ctrl Pts',(-20.5858865449141,20.2367907730763,
18.3773663502096));
#202904=CARTESIAN_POINT('Ctrl Pts',(-20.5889988843644,20.231151764664,18.3769805773689));
#202905=CARTESIAN_POINT('Ctrl Pts',(-20.5960893284217,20.2181653992436,
18.3760922473868));
#202906=CARTESIAN_POINT('Ctrl Pts',(-20.6000497474464,20.2108085543667,
18.3755890666401));
#202907=CARTESIAN_POINT('Ctrl Pts',(-20.6105050996627,20.1911082361159,
18.3742417105235));
#202908=CARTESIAN_POINT('Ctrl Pts',(-20.6169216854225,20.1787238529215,
18.3733947830993));
#202909=CARTESIAN_POINT('Ctrl Pts',(-20.6608289641559,20.0918901009572,
18.3674560923311));
#202910=CARTESIAN_POINT('Ctrl Pts',(-20.6940057709894,20.0153675122898,
18.3622160718341));
#202911=CARTESIAN_POINT('Ctrl Pts',(-20.7225806168679,19.9371102741439,
18.3568545763217));
#202912=CARTESIAN_POINT('',(-20.8509999550631,19.2114361911346,18.8870728602009));
#202913=CARTESIAN_POINT('Ctrl Pts',(-20.7225805905512,19.9371103462167,
18.1318063719887));
#202914=CARTESIAN_POINT('Ctrl Pts',(-20.7014550076874,19.9949664617037,
18.1356559894487));
#202915=CARTESIAN_POINT('Ctrl Pts',(-20.6778120315239,20.0518801287616,
18.1395843992343));
#202916=CARTESIAN_POINT('Ctrl Pts',(-20.5968950914491,20.224934280491,18.1519521847457));
#202917=CARTESIAN_POINT('Ctrl Pts',(-20.5314380472283,20.3369012678676,
18.1605861116263));
#202918=CARTESIAN_POINT('Ctrl Pts',(-20.4404259146217,20.4642090398079,
18.1708509745924));
#202919=CARTESIAN_POINT('Ctrl Pts',(-20.4242556921629,20.485934535488,18.1726189867731));
#202920=CARTESIAN_POINT('Ctrl Pts',(-20.3724969077827,20.5527588064822,
18.1780958165893));
#202921=CARTESIAN_POINT('Ctrl Pts',(-20.3354836828427,20.5967272765699,
18.1817564171383));
#202922=CARTESIAN_POINT('Ctrl Pts',(-20.2907363266949,20.6456915335486,
18.1858494298112));
#202923=CARTESIAN_POINT('Ctrl Pts',(-20.2847071114606,20.6522061782003,
18.1863943426289));
#202924=CARTESIAN_POINT('Ctrl Pts',(-20.2755483185451,20.6619783533334,
18.1872119820656));
#202925=CARTESIAN_POINT('Ctrl Pts',(-20.2724490850876,20.66526401101,18.1874869371576));
#202926=CARTESIAN_POINT('Ctrl Pts',(-20.2668839605058,20.6711261870312,
18.1879775404821));
#202927=CARTESIAN_POINT('Ctrl Pts',(-20.2644220611377,20.6737064072546,
18.1881934883807));
#202928=CARTESIAN_POINT('Ctrl Pts',(-20.2590779310063,20.6792791171241,
18.1886599050395));
#202929=CARTESIAN_POINT('Ctrl Pts',(-20.2561934168391,20.6822693376259,
18.1889101918702));
#202930=CARTESIAN_POINT('Ctrl Pts',(-20.2481154104312,20.6905941854478,
18.1896071070354));
#202931=CARTESIAN_POINT('Ctrl Pts',(-20.2429024933695,20.695909996921,18.1900522479129));
#202932=CARTESIAN_POINT('Ctrl Pts',(-20.2125438421952,20.7265429247764,
18.1926189565747));
#202933=CARTESIAN_POINT('Ctrl Pts',(-20.1867876621509,20.7512501739136,
18.1946953023093));
#202934=CARTESIAN_POINT('Ctrl Pts',(-20.10214195486,20.8284351276772,18.2012502157399));
#202935=CARTESIAN_POINT('Ctrl Pts',(-20.0409377282773,20.8782805742249,
18.205591708788));
#202936=CARTESIAN_POINT('Ctrl Pts',(-19.903360404184,20.978082920464,18.2148611437696));
#202937=CARTESIAN_POINT('Ctrl Pts',(-19.8262564389236,21.0267537140959,
18.2197680932191));
#202938=CARTESIAN_POINT('Ctrl Pts',(-19.6529377496387,21.1211131645764,
18.2306138081417));
#202939=CARTESIAN_POINT('Ctrl Pts',(-19.5559369742601,21.164815304497,18.2365764534918));
#202940=CARTESIAN_POINT('Ctrl Pts',(-19.4428143753893,21.205860931257,18.2436280282627));
#202941=CARTESIAN_POINT('Ctrl Pts',(-19.4295076127225,21.210539221949,18.2444588019421));
#202942=CARTESIAN_POINT('Ctrl Pts',(-19.408202400471,21.2177911451676,18.2457914076723));
#202943=CARTESIAN_POINT('Ctrl Pts',(-19.4002335180901,21.2204507889951,
18.246290394381));
#202944=CARTESIAN_POINT('Ctrl Pts',(-19.3861205857683,21.2250678539145,
18.247175151934));
#202945=CARTESIAN_POINT('Ctrl Pts',(-19.3799829936524,21.2270447785321,
18.2475602743498));
#202946=CARTESIAN_POINT('Ctrl Pts',(-19.3672397023328,21.231085238857,18.2483606554466));
#202947=CARTESIAN_POINT('Ctrl Pts',(-19.3606327325623,21.2331444828624,
18.2487760498115));
#202948=CARTESIAN_POINT('Ctrl Pts',(-19.3435839202667,21.238366636684,18.2498490913408));
#202949=CARTESIAN_POINT('Ctrl Pts',(-19.333127606431,21.2414812581307,18.2505083099329));
#202950=CARTESIAN_POINT('Ctrl Pts',(-19.2888347032104,21.2543028617376,
18.2533057235464));
#202951=CARTESIAN_POINT('Ctrl Pts',(-19.2547844205216,21.263245474215,18.2554685783143));
#202952=CARTESIAN_POINT('Ctrl Pts',(-19.1649549720866,21.2844578494643,
18.2612100587309));
#202953=CARTESIAN_POINT('Ctrl Pts',(-19.1088774663373,21.2953261788324,
18.2648303699799));
#202954=CARTESIAN_POINT('Ctrl Pts',(-18.9020410036757,21.3267959593207,
18.2782996189891));
#202955=CARTESIAN_POINT('Ctrl Pts',(-18.7496251547766,21.3333994417114,
18.2884871436087));
#202956=CARTESIAN_POINT('Ctrl Pts',(-18.5753870926614,21.3221696184504,
18.299891168646));
#202957=CARTESIAN_POINT('Ctrl Pts',(-18.5529584413561,21.3203646475768,
18.301353571541));
#202958=CARTESIAN_POINT('Ctrl Pts',(-18.4794374827478,21.3132666418875,
18.3061210164816));
#202959=CARTESIAN_POINT('Ctrl Pts',(-18.428504485824,21.3064714354772,18.3093821980804));
#202960=CARTESIAN_POINT('Ctrl Pts',(-18.3701013410559,21.2965044462548,
18.3130364374369));
#202961=CARTESIAN_POINT('Ctrl Pts',(-18.3623450304538,21.2951361801352,
18.3135199892109));
#202962=CARTESIAN_POINT('Ctrl Pts',(-18.3499902583087,21.2928855489414,
18.3142872263364));
#202963=CARTESIAN_POINT('Ctrl Pts',(-18.3453868620607,21.2920311748256,
18.3145724345939));
#202964=CARTESIAN_POINT('Ctrl Pts',(-18.3372558422888,21.2904941651123,
18.3150749786665));
#202965=CARTESIAN_POINT('Ctrl Pts',(-18.3337270742182,21.2898178118939,
18.3152926681362));
#202966=CARTESIAN_POINT('Ctrl Pts',(-18.3262701896523,21.2883688714348,
18.3157518034549));
#202967=CARTESIAN_POINT('Ctrl Pts',(-18.3223425449182,21.2875941265784,
18.3159931246794));
#202968=CARTESIAN_POINT('Ctrl Pts',(-18.3117895442108,21.2854813847912,
18.3166401999731));
#202969=CARTESIAN_POINT('Ctrl Pts',(-18.3051682946728,21.2841227788403,
18.3170447937068));
#202970=CARTESIAN_POINT('Ctrl Pts',(-18.2728640481678,21.2773329209507,
18.3190124156881));
#202971=CARTESIAN_POINT('Ctrl Pts',(-18.2472758454926,21.2714557375733,
18.3205513730988));
#202972=CARTESIAN_POINT('Ctrl Pts',(-18.1742917918238,21.2532569176944,
18.3249016689608));
#202973=CARTESIAN_POINT('Ctrl Pts',(-18.1272033909768,21.2397644274806,
18.3276607572441));
#202974=CARTESIAN_POINT('Ctrl Pts',(-17.9887178939118,21.1948294535513,
18.3357444543911));
#202975=CARTESIAN_POINT('Ctrl Pts',(-17.8989593561815,21.1587508293806,
18.3409474140977));
#202976=CARTESIAN_POINT('Ctrl Pts',(-17.6850124696732,21.0552363196111,
18.3538802746827));
#202977=CARTESIAN_POINT('Ctrl Pts',(-17.5645233672985,20.9812822697259,
18.3616599362714));
#202978=CARTESIAN_POINT('Ctrl Pts',(-17.4409209454358,20.8872576057647,
18.3707580344716));
#202979=CARTESIAN_POINT('Ctrl Pts',(-17.4296412792304,20.8784955217034,
18.371599137892));
#202980=CARTESIAN_POINT('Ctrl Pts',(-17.4118288561947,20.864367446892,18.3729451913875));
#202981=CARTESIAN_POINT('Ctrl Pts',(-17.4052379645834,20.8590752100642,
18.3734472039031));
#202982=CARTESIAN_POINT('Ctrl Pts',(-17.3936689194967,20.8496711936877,
18.3743354788066));
#202983=CARTESIAN_POINT('Ctrl Pts',(-17.3886775236237,20.8455758225045,
18.3747210758297));
#202984=CARTESIAN_POINT('Ctrl Pts',(-17.3783915517784,20.8370572964553,
18.3755206239967));
#202985=CARTESIAN_POINT('Ctrl Pts',(-17.373099712929,20.8326309700862,18.3759347018494));
#202986=CARTESIAN_POINT('Ctrl Pts',(-17.3595698259514,20.8212011088449,
18.3770004946254));
#202987=CARTESIAN_POINT('Ctrl Pts',(-17.351363702253,20.8141602463947,18.3776537406161));
#202988=CARTESIAN_POINT('Ctrl Pts',(-17.3173217825595,20.7844964588721,
18.3803926126732));
#202989=CARTESIAN_POINT('Ctrl Pts',(-17.2919856265056,20.7613104874583,
18.3825016300847));
#202990=CARTESIAN_POINT('Ctrl Pts',(-17.2274341787727,20.699285469669,18.3880662112844));
#202991=CARTESIAN_POINT('Ctrl Pts',(-17.1891558159554,20.6595129739667,
18.3915603348426));
#202992=CARTESIAN_POINT('Ctrl Pts',(-17.079712317872,20.5365198516453,18.4021433884306));
#202993=CARTESIAN_POINT('Ctrl Pts',(-17.0134042554094,20.4492315744595,
18.4093806639699));
#202994=CARTESIAN_POINT('Ctrl Pts',(-16.9252676750691,20.3123725070272,
18.4201335400683));
#202995=CARTESIAN_POINT('Ctrl Pts',(-16.8980924733817,20.2664515219804,
18.423649098732));
#202996=CARTESIAN_POINT('Ctrl Pts',(-16.8666535691045,20.2084298603262,
18.427943873464));
#202997=CARTESIAN_POINT('Ctrl Pts',(-16.8607268113086,20.1972538157768,
18.4287645453795));
#202998=CARTESIAN_POINT('Ctrl Pts',(-16.8303567746165,20.1387237151428,
18.4330260693232));
#202999=CARTESIAN_POINT('Ctrl Pts',(-16.8076055108233,20.0905078891366,
18.4364135828855));
#203000=CARTESIAN_POINT('Ctrl Pts',(-16.7832770591629,20.0334627575651,
18.4402391919341));
#203001=CARTESIAN_POINT('Ctrl Pts',(-16.7799070889915,20.0254236493611,
18.4407741885624));
#203002=CARTESIAN_POINT('Ctrl Pts',(-16.7748794475646,20.0132192675484,
18.4415798921587));
#203003=CARTESIAN_POINT('Ctrl Pts',(-16.7731852414488,20.0090692800151,
18.4418527339967));
#203004=CARTESIAN_POINT('Ctrl Pts',(-16.7701676973725,20.0016101367109,
18.4423410696028));
#203005=CARTESIAN_POINT('Ctrl Pts',(-16.7688395290751,19.9983030072413,
18.4425568512549));
#203006=CARTESIAN_POINT('Ctrl Pts',(-16.7659715776412,19.991109353844,18.4430246303433));
#203007=CARTESIAN_POINT('Ctrl Pts',(-16.7644349577649,19.987221630893,18.44327643657));
#203008=CARTESIAN_POINT('Ctrl Pts',(-16.7601507300588,19.9762876956346,
18.4439818872953));
#203009=CARTESIAN_POINT('Ctrl Pts',(-16.7574293183007,19.969231192774,18.4444339847251));
#203010=CARTESIAN_POINT('Ctrl Pts',(-16.7413800264958,19.9269424347717,
18.4471252075736));
#203011=CARTESIAN_POINT('Ctrl Pts',(-16.728955722396,19.8913717868833,18.4493138265337));
#203012=CARTESIAN_POINT('Ctrl Pts',(-16.6911827020441,19.7731849057294,
18.4563989895548));
#203013=CARTESIAN_POINT('Ctrl Pts',(-16.669939913382,19.6893437057548,18.4611316698816));
#203014=CARTESIAN_POINT('Ctrl Pts',(-16.6211081375412,19.4311652019751,
18.4754304050701));
#203015=CARTESIAN_POINT('Ctrl Pts',(-16.6101154567431,19.2545031734588,
18.4849065781047));
#203016=CARTESIAN_POINT('Ctrl Pts',(-16.6225836427218,19.055643226487,18.4964854424401));
#203017=CARTESIAN_POINT('Ctrl Pts',(-16.624390123769,19.032784202349,18.4978288338834));
#203018=CARTESIAN_POINT('Ctrl Pts',(-16.6274730760298,19.0004667381701,
18.4997473952577));
#203019=CARTESIAN_POINT('Ctrl Pts',(-16.6284427813954,18.9909801590596,
18.5003129355149));
#203020=CARTESIAN_POINT('Ctrl Pts',(-16.6301231906189,18.9755707061212,
18.5012355224035));
#203021=CARTESIAN_POINT('Ctrl Pts',(-16.6307949002812,18.9696436475599,
18.5015913369993));
#203022=CARTESIAN_POINT('Ctrl Pts',(-16.632253958639,18.9572379663657,18.5023381074554));
#203023=CARTESIAN_POINT('Ctrl Pts',(-16.6330462329962,18.9507599963057,
18.5027292151583));
#203024=CARTESIAN_POINT('Ctrl Pts',(-16.63500344822,18.9353487050685,18.5036624825223));
#203025=CARTESIAN_POINT('Ctrl Pts',(-16.6361954772838,18.926419007431,18.5042054927138));
#203026=CARTESIAN_POINT('Ctrl Pts',(-16.6404094781528,18.8963174553767,
18.5060437008792));
#203027=CARTESIAN_POINT('Ctrl Pts',(-16.6436951880649,18.8751843994187,
18.5073472017004));
#203028=CARTESIAN_POINT('Ctrl Pts',(-16.6633755087638,18.7601170653344,
18.5145178641753));
#203029=CARTESIAN_POINT('Ctrl Pts',(-16.6857800060727,18.6673348307803,
18.5205745432654));
#203030=CARTESIAN_POINT('Ctrl Pts',(-16.7654990620338,18.4136301285492,
18.5378562431451));
#203031=CARTESIAN_POINT('Ctrl Pts',(-16.8361232310038,18.2576609675694,
18.5493674729598));
#203032=CARTESIAN_POINT('Ctrl Pts',(-16.9437230669628,18.0805396478754,
18.5625930779529));
#203033=CARTESIAN_POINT('Ctrl Pts',(-16.9635622741014,18.0497150493651,
18.5648981586729));
#203034=CARTESIAN_POINT('Ctrl Pts',(-16.9882081863394,18.0135231417081,
18.5675945047978));
#203035=CARTESIAN_POINT('Ctrl Pts',(-16.9922530497112,18.0076474135751,
18.5680319258315));
#203036=CARTESIAN_POINT('Ctrl Pts',(-16.9989034819625,17.9980905184959,
18.5687427051508));
#203037=CARTESIAN_POINT('Ctrl Pts',(-17.0014912130962,17.9943970896796,
18.5690172292113));
#203038=CARTESIAN_POINT('Ctrl Pts',(-17.0061461442436,17.9877981491884,
18.5695073681991));
#203039=CARTESIAN_POINT('Ctrl Pts',(-17.0082088932235,17.9848895763197,
18.5697232803919));
#203040=CARTESIAN_POINT('Ctrl Pts',(-17.0126939869186,17.978599126359,18.570189966734));
#203041=CARTESIAN_POINT('Ctrl Pts',(-17.0151189457656,17.9752191836336,
18.5704405570921));
#203042=CARTESIAN_POINT('Ctrl Pts',(-17.021925507103,17.965790896765,18.5711391748603));
#203043=CARTESIAN_POINT('Ctrl Pts',(-17.0263292270764,17.9597584905057,
18.5715857030078));
#203044=CARTESIAN_POINT('Ctrl Pts',(-17.0521852350735,17.924730579548,18.5741766312995));
#203045=CARTESIAN_POINT('Ctrl Pts',(-17.0743451903466,17.8962619317625,
18.5762748056793));
#203046=CARTESIAN_POINT('Ctrl Pts',(-17.1481437640279,17.806295273004,18.5829305490586));
#203047=CARTESIAN_POINT('Ctrl Pts',(-17.2025586858378,17.7471609077914,
18.587346139373));
#203048=CARTESIAN_POINT('Ctrl Pts',(-17.3932703468835,17.5622152803035,
18.6018276925815));
#203049=CARTESIAN_POINT('Ctrl Pts',(-17.5426891605687,17.451221746326,18.6117428572409));
#203050=CARTESIAN_POINT('Ctrl Pts',(-17.7239879405533,17.3503403016593,
18.6238093829938));
#203051=CARTESIAN_POINT('Ctrl Pts',(-17.7434955031188,17.3398827774709,
18.6251068105974));
#203052=CARTESIAN_POINT('Ctrl Pts',(-17.7706835638669,17.3258522427365,
18.6269153199065));
#203053=CARTESIAN_POINT('Ctrl Pts',(-17.7782273326181,17.3220163505299,
18.6274171446793));
#203054=CARTESIAN_POINT('Ctrl Pts',(-17.7912290431025,17.3155029996447,
18.6282821712426));
#203055=CARTESIAN_POINT('Ctrl Pts',(-17.796675928187,17.3128036090174,18.628644600817));
#203056=CARTESIAN_POINT('Ctrl Pts',(-17.8079245431053,17.3072891941951,
18.6293931859976));
#203057=CARTESIAN_POINT('Ctrl Pts',(-17.8137276540915,17.3044771462345,
18.6297794405168));
#203058=CARTESIAN_POINT('Ctrl Pts',(-17.8272543474449,17.2979985838706,
18.6306799647255));
#203059=CARTESIAN_POINT('Ctrl Pts',(-17.8349874330673,17.294352276059,18.6311949286769));
#203060=CARTESIAN_POINT('Ctrl Pts',(-17.8597787799449,17.2828456948266,
18.6328464176771));
#203061=CARTESIAN_POINT('Ctrl Pts',(-17.8769192795361,17.2751657175578,
18.6339891180636));
#203062=CARTESIAN_POINT('Ctrl Pts',(-17.9628696376711,17.2380200536409,
18.6397249928209));
#203063=CARTESIAN_POINT('Ctrl Pts',(-18.0330990949681,17.2119933227832,
18.644433032704));
#203064=CARTESIAN_POINT('Ctrl Pts',(-18.2084873225002,17.1573750587722,
18.6562343147341));
#203065=CARTESIAN_POINT('Ctrl Pts',(-18.3147562448931,17.1330755144151,
18.6634279804527));
#203066=CARTESIAN_POINT('Ctrl Pts',(-18.5410782417617,17.0993978681545,
18.6785444460428));
#203067=CARTESIAN_POINT('Ctrl Pts',(-18.6610446929986,17.0918571167076,
18.6864394334074));
#203068=CARTESIAN_POINT('Ctrl Pts',(-18.7905255665961,17.0947333931917,
18.6944387466851));
#203069=CARTESIAN_POINT('Ctrl Pts',(-18.8000345575661,17.0950087581136,
18.6950230991984));
#203070=CARTESIAN_POINT('Ctrl Pts',(-18.8141225778557,17.0955117856868,
18.6958839116011));
#203071=CARTESIAN_POINT('Ctrl Pts',(-18.818703091444,17.0956902355463,18.6961630189385));
#203072=CARTESIAN_POINT('Ctrl Pts',(-18.8268519529105,17.0960342142993,
18.6966581391539));
#203073=CARTESIAN_POINT('Ctrl Pts',(-18.8304204901521,17.0961938978762,
18.6968744747662));
#203074=CARTESIAN_POINT('Ctrl Pts',(-18.8380920598155,17.096556641007,18.6973384937323));
#203075=CARTESIAN_POINT('Ctrl Pts',(-18.8421948983607,17.0967626103168,
18.6975860123356));
#203076=CARTESIAN_POINT('Ctrl Pts',(-18.8535187886543,17.0973641377088,
18.6982674533202));
#203077=CARTESIAN_POINT('Ctrl Pts',(-18.8607385313378,17.0977847607705,
18.6986999936056));
#203078=CARTESIAN_POINT('Ctrl Pts',(-18.9002851624277,17.100292153106,18.7010594048153));
#203079=CARTESIAN_POINT('Ctrl Pts',(-18.9325649386611,17.1030838265953,
18.7029491691305));
#203080=CARTESIAN_POINT('Ctrl Pts',(-19.1266009342844,17.1243620946157,
18.7141585654862));
#203081=CARTESIAN_POINT('Ctrl Pts',(-19.2858615262963,17.1607185577273,
18.7227633917145));
#203082=CARTESIAN_POINT('Ctrl Pts',(-19.549573589651,17.2539143043239,18.7380750868553));
#203083=CARTESIAN_POINT('Ctrl Pts',(-19.6563256189776,17.3019020740949,
18.7445985568056));
#203084=CARTESIAN_POINT('Ctrl Pts',(-19.7721868663751,17.365979864426,18.7523548877149));
#203085=CARTESIAN_POINT('Ctrl Pts',(-19.7857238043305,17.3736627173271,
18.7532718945608));
#203086=CARTESIAN_POINT('Ctrl Pts',(-19.8061730604815,17.385568678129,18.7546741709939));
#203087=CARTESIAN_POINT('Ctrl Pts',(-19.8131480780999,17.3896834417822,
18.7551555215593));
#203088=CARTESIAN_POINT('Ctrl Pts',(-19.8254397220556,17.3970300326623,
18.7560092619945));
#203089=CARTESIAN_POINT('Ctrl Pts',(-19.8307660606806,17.400245484295,18.7563810508131));
#203090=CARTESIAN_POINT('Ctrl Pts',(-19.8420027225034,17.4070966996114,
18.7571693257224));
#203091=CARTESIAN_POINT('Ctrl Pts',(-19.8479094886132,17.4107381302653,
18.7575860172026));
#203092=CARTESIAN_POINT('Ctrl Pts',(-19.8599606508176,17.4182495036909,
18.7584409698363));
#203093=CARTESIAN_POINT('Ctrl Pts',(-19.866103246299,17.4221221487008,18.758879327386));
#203094=CARTESIAN_POINT('Ctrl Pts',(-19.8812447569507,17.4317774489148,
18.759966334535));
#203095=CARTESIAN_POINT('Ctrl Pts',(-19.8902199257273,17.4375968040521,
18.7606163438544));
#203096=CARTESIAN_POINT('Ctrl Pts',(-19.996728812433,17.5078076929853,18.7683988411112));
#203097=CARTESIAN_POINT('Ctrl Pts',(-20.0887969077889,17.5800905647174,
18.7758355776126));
#203098=CARTESIAN_POINT('Ctrl Pts',(-20.310417376706,17.7858558121241,18.7955807218107));
#203099=CARTESIAN_POINT('Ctrl Pts',(-20.4292197414015,17.9294541777997,
18.808144404582));
#203100=CARTESIAN_POINT('Ctrl Pts',(-20.535338539805,18.0987630240731,18.8205838211335));
#203101=CARTESIAN_POINT('Ctrl Pts',(-20.542776691332,18.1109006719478,18.8214632787622));
#203102=CARTESIAN_POINT('Ctrl Pts',(-20.5529510031847,18.1278854172129,
18.8226759152318));
#203103=CARTESIAN_POINT('Ctrl Pts',(-20.5557911451072,18.1326693565273,
18.8230154997651));
#203104=CARTESIAN_POINT('Ctrl Pts',(-20.5603198777447,18.1403665233724,
18.8235586561472));
#203105=CARTESIAN_POINT('Ctrl Pts',(-20.5620204116266,18.1432726414643,
18.8237629951947));
#203106=CARTESIAN_POINT('Ctrl Pts',(-20.5655581675288,18.1493516959139,
18.8241888840266));
#203107=CARTESIAN_POINT('Ctrl Pts',(-20.567394086377,18.1525253584206,18.8244103446589));
#203108=CARTESIAN_POINT('Ctrl Pts',(-20.5718154178768,18.1602143122068,
18.8249447950763));
#203109=CARTESIAN_POINT('Ctrl Pts',(-20.574392468853,18.1647344344013,18.8252572462968));
#203110=CARTESIAN_POINT('Ctrl Pts',(-20.5833492816421,18.1805800851206,
18.8263466679732));
#203111=CARTESIAN_POINT('Ctrl Pts',(-20.5896415238493,18.1919550940256,
18.8271182177777));
#203112=CARTESIAN_POINT('Ctrl Pts',(-20.6261717186448,18.2594542348069,
18.8316391787254));
#203113=CARTESIAN_POINT('Ctrl Pts',(-20.6539696182429,18.3168683694867,
18.8352523704476));
#203114=CARTESIAN_POINT('Ctrl Pts',(-20.7670746929877,18.5801751691126,
18.8511806925627));
#203115=CARTESIAN_POINT('Ctrl Pts',(-20.8221439376655,18.7974839958582,
18.8627824789036));
#203116=CARTESIAN_POINT('Ctrl Pts',(-20.8447697705718,19.0464467519669,
18.877249995478));
#203117=CARTESIAN_POINT('Ctrl Pts',(-20.8467072345963,19.0735415067363,
18.8788370064226));
#203118=CARTESIAN_POINT('Ctrl Pts',(-20.8486554028962,19.1108703059235,
18.8810435528669));
#203119=CARTESIAN_POINT('Ctrl Pts',(-20.8491140969093,19.1210790339432,
18.8816490613351));
#203120=CARTESIAN_POINT('Ctrl Pts',(-20.8497282755774,19.1373794130681,
18.8826193142311));
#203121=CARTESIAN_POINT('Ctrl Pts',(-20.8499314061028,19.1434691894635,
18.882982561869));
#203122=CARTESIAN_POINT('Ctrl Pts',(-20.8502862993201,19.1556923162535,
18.8837132236441));
#203123=CARTESIAN_POINT('Ctrl Pts',(-20.8504376956191,19.1618256173907,
18.8840806456684));
#203124=CARTESIAN_POINT('Ctrl Pts',(-20.8507174560923,19.1755831175595,
18.8849066150619));
#203125=CARTESIAN_POINT('Ctrl Pts',(-20.8508312920298,19.18320749748,18.8853656133632));
#203126=CARTESIAN_POINT('Ctrl Pts',(-20.8509693631967,19.1977001098008,
18.8862405120949));
#203127=CARTESIAN_POINT('Ctrl Pts',(-20.8510013701644,19.2045681711671,
18.8866561616126));
#203128=CARTESIAN_POINT('Ctrl Pts',(-20.8509999550631,19.2114361911346,
18.8870728602009));
#203129=CARTESIAN_POINT('Ctrl Pts',(-20.8509999552301,19.2114353802296,
18.8870728110014));
#203130=CARTESIAN_POINT('Ctrl Pts',(-20.8509977625579,19.2220970650987,
18.8877196798475));
#203131=CARTESIAN_POINT('Ctrl Pts',(-20.850915028038,19.2327584644317,18.8883690662257));
#203132=CARTESIAN_POINT('Ctrl Pts',(-20.850420668131,19.2650373055968,18.8903430083297));
#203133=CARTESIAN_POINT('Ctrl Pts',(-20.8497584121093,19.286648942304,18.8916752809909));
#203134=CARTESIAN_POINT('Ctrl Pts',(-20.8411876622882,19.4730331322725,
18.903259385164));
#203135=CARTESIAN_POINT('Ctrl Pts',(-20.8143762766218,19.6363439341123,
18.9141120151009));
#203136=CARTESIAN_POINT('Ctrl Pts',(-20.7551361081569,19.8428126233419,
18.9283024366599));
#203137=CARTESIAN_POINT('Ctrl Pts',(-20.739687226211,19.8902608224799,18.9315919516632));
#203138=CARTESIAN_POINT('Ctrl Pts',(-20.7225805923249,19.9371103413593,
18.9348455557956));
#203139=CARTESIAN_POINT('Origin',(-18.734,19.211,0.));
#203140=CARTESIAN_POINT('',(-20.7225806070201,19.9371103011137,19.9537492499338));
#203141=CARTESIAN_POINT('',(-20.7225805741668,19.9371103910883,19.7345261348292));
#203142=CARTESIAN_POINT('',(-20.7225806064498,19.9371103026755,0.));
#203143=CARTESIAN_POINT('',(-20.8479141177977,19.2118284581339,19.910995664247));
#203144=CARTESIAN_POINT('Ctrl Pts',(-20.7225806070201,19.9371103011137,
19.9537492499338));
#203145=CARTESIAN_POINT('Ctrl Pts',(-20.7405653140382,19.8878560217788,
19.9507625358576));
#203146=CARTESIAN_POINT('Ctrl Pts',(-20.7567162132681,19.8379441465122,
19.9478475669179));
#203147=CARTESIAN_POINT('Ctrl Pts',(-20.8240164289173,19.6001371512545,
19.9342646615474));
#203148=CARTESIAN_POINT('Ctrl Pts',(-20.8509329967896,19.4064030179224,
19.9239833448394));
#203149=CARTESIAN_POINT('Ctrl Pts',(-20.8509998750784,19.2117272674118,
19.9127739856851));
#203150=CARTESIAN_POINT('Ctrl Pts',(-20.7202231500468,19.93627084876,19.1554367712949));
#203151=CARTESIAN_POINT('Ctrl Pts',(-20.632847054901,20.1806249108887,19.1710019318661));
#203152=CARTESIAN_POINT('Ctrl Pts',(-20.1480309705507,21.030328314946,19.2289590279977));
#203153=CARTESIAN_POINT('Ctrl Pts',(-18.3741968251021,21.6882711019052,
19.3293080596899));
#203154=CARTESIAN_POINT('Ctrl Pts',(-16.4562524007973,20.2493623486039,
19.4564838663713));
#203155=CARTESIAN_POINT('Ctrl Pts',(-16.6280000239015,17.8578205442181,
19.5836596730528));
#203156=CARTESIAN_POINT('Ctrl Pts',(-18.7318719156385,16.7077369880417,
19.7108354797341));
#203157=CARTESIAN_POINT('Ctrl Pts',(-20.5383022142055,17.6912382698633,
19.8199301623757));
#203158=CARTESIAN_POINT('Ctrl Pts',(-20.8463944722286,18.8061996577397,
19.8866329094569));
#203159=CARTESIAN_POINT('Ctrl Pts',(-20.8478239854299,19.2118314138296,
19.9109437209775));
#203160=CARTESIAN_POINT('Ctrl Pts',(-20.7225805923249,19.9371103413593,
18.9348455557956));
#203161=CARTESIAN_POINT('Ctrl Pts',(-20.710360467218,19.9705772984304,18.9371697681339));
#203162=CARTESIAN_POINT('Ctrl Pts',(-20.6972943982248,20.0037387601119,
18.9394755308538));
#203163=CARTESIAN_POINT('Ctrl Pts',(-20.6687906446562,20.0710444200022,
18.9441406592123));
#203164=CARTESIAN_POINT('Ctrl Pts',(-20.6532742864404,20.1051352555742,
18.9464955566324));
#203165=CARTESIAN_POINT('Ctrl Pts',(-20.6335516713709,20.1455851764302,
18.9492646624661));
#203166=CARTESIAN_POINT('Ctrl Pts',(-20.6302064116756,20.152353946439,18.9497271749787));
#203167=CARTESIAN_POINT('Ctrl Pts',(-20.6249540245575,20.162839970243,18.9504421783014));
#203168=CARTESIAN_POINT('Ctrl Pts',(-20.6230720245406,20.1665696409664,
18.9506961922967));
#203169=CARTESIAN_POINT('Ctrl Pts',(-20.6195639348222,20.17347096097,18.95116562712));
#203170=CARTESIAN_POINT('Ctrl Pts',(-20.6179408903305,20.1766440467623,
18.9513812283854));
#203171=CARTESIAN_POINT('Ctrl Pts',(-20.6142568256493,20.1838018268405,
18.9518670574669));
#203172=CARTESIAN_POINT('Ctrl Pts',(-20.6121911544154,20.1877840667376,
18.9521369882068));
#203173=CARTESIAN_POINT('Ctrl Pts',(-20.6060667987521,20.1994994558908,
18.9529301232858));
#203174=CARTESIAN_POINT('Ctrl Pts',(-20.6019728447992,20.2072141990175,
18.9534511552968));
#203175=CARTESIAN_POINT('Ctrl Pts',(-20.5723566895963,20.2621990772766,
18.95715723626));
#203176=CARTESIAN_POINT('Ctrl Pts',(-20.5450888442467,20.3085122120635,
18.9602394581677));
#203177=CARTESIAN_POINT('Ctrl Pts',(-20.4252331004243,20.4954252059314,
18.9727226983674));
#203178=CARTESIAN_POINT('Ctrl Pts',(-20.3178045746723,20.6257750065153,
18.9815807144511));
#203179=CARTESIAN_POINT('Ctrl Pts',(-20.1529709502013,20.7831835048041,
18.9942099302935));
#203180=CARTESIAN_POINT('Ctrl Pts',(-20.1081622153545,20.8224952531611,
18.9975588869045));
#203181=CARTESIAN_POINT('Ctrl Pts',(-20.0334871111794,20.8826278599759,
19.0030654766779));
#203182=CARTESIAN_POINT('Ctrl Pts',(-20.0046373039412,20.9046608470138,
19.0051760294489));
#203183=CARTESIAN_POINT('Ctrl Pts',(-19.9686169170661,20.9307316196453,
19.0077975438664));
#203184=CARTESIAN_POINT('Ctrl Pts',(-19.9619696259046,20.9354843781678,
19.0082807642692));
#203185=CARTESIAN_POINT('Ctrl Pts',(-19.9490943378091,20.9445779124438,
19.0092157415624));
#203186=CARTESIAN_POINT('Ctrl Pts',(-19.942870173226,20.9489239138337,19.0096672896238));
#203187=CARTESIAN_POINT('Ctrl Pts',(-19.9365819733175,20.9532645034312,
19.0101230790902));
#203188=CARTESIAN_POINT('Ctrl Pts',(-19.9365411161683,20.9532927039936,
19.0101260405339));
#203189=CARTESIAN_POINT('Ctrl Pts',(-19.9364577119075,20.9533502672387,
19.0101320858799));
#203190=CARTESIAN_POINT('Ctrl Pts',(-19.9364151647884,20.9533796297475,
19.0101351697812));
#203191=CARTESIAN_POINT('Ctrl Pts',(-19.936328266968,20.9534395947502,19.0101414682732));
#203192=CARTESIAN_POINT('Ctrl Pts',(-19.9362839159617,20.9534701972554,
19.0101446828844));
#203193=CARTESIAN_POINT('Ctrl Pts',(-19.936193284958,20.9535327281756,19.0101512518811));
#203194=CARTESIAN_POINT('Ctrl Pts',(-19.9361470049187,20.9535646563977,
19.0101546062679));
#203195=CARTESIAN_POINT('Ctrl Pts',(-19.9360523782072,20.9536299330311,
19.0101614647866));
#203196=CARTESIAN_POINT('Ctrl Pts',(-19.9360040315621,20.9536632811757,
19.0101649689146));
#203197=CARTESIAN_POINT('Ctrl Pts',(-19.9359051206447,20.9537315010468,
19.0101721378536));
#203198=CARTESIAN_POINT('Ctrl Pts',(-19.935854556117,20.9537663726712,19.0101758026809));
#203199=CARTESIAN_POINT('Ctrl Pts',(-19.935751041673,20.9538377543462,19.0101833051708));
#203200=CARTESIAN_POINT('Ctrl Pts',(-19.9356980917437,20.9538742640926,
19.0101871428318));
#203201=CARTESIAN_POINT('Ctrl Pts',(-19.9355896214927,20.9539490486151,
19.01019500439));
#203202=CARTESIAN_POINT('Ctrl Pts',(-19.9355341008688,20.9539873232462,
19.0101990283062));
#203203=CARTESIAN_POINT('Ctrl Pts',(-19.9354202827788,20.9540657787762,
19.0102072773288));
#203204=CARTESIAN_POINT('Ctrl Pts',(-19.9353619851864,20.9541059593616,
19.0102115024412));
#203205=CARTESIAN_POINT('Ctrl Pts',(-19.9352423834067,20.9541883839248,
19.0102201704975));
#203206=CARTESIAN_POINT('Ctrl Pts',(-19.9351810789387,20.9542306276401,
19.0102246134582));
#203207=CARTESIAN_POINT('Ctrl Pts',(-19.9350552059521,20.954317354472,19.0102337358588));
#203208=CARTESIAN_POINT('Ctrl Pts',(-19.9349906371787,20.9543618372435,
19.0102384153131));
#203209=CARTESIAN_POINT('Ctrl Pts',(-19.9348579461057,20.9544532400145,
19.0102480316671));
#203210=CARTESIAN_POINT('Ctrl Pts',(-19.9347898236244,20.9545001595418,
19.0102529685753));
#203211=CARTESIAN_POINT('Ctrl Pts',(-19.9346496988297,20.9545966587324,
19.0102631234702));
#203212=CARTESIAN_POINT('Ctrl Pts',(-19.934577696169,20.9546462379462,19.0102683414766));
#203213=CARTESIAN_POINT('Ctrl Pts',(-19.9344294410399,20.9547483091474,
19.0102790853632));
#203214=CARTESIAN_POINT('Ctrl Pts',(-19.9343531881439,20.9548008006314,
19.0102846112681));
#203215=CARTESIAN_POINT('Ctrl Pts',(-19.9341960107911,20.9549089842453,
19.0102960014956));
#203216=CARTESIAN_POINT('Ctrl Pts',(-19.93411508598,20.9549646756897,19.0103018658366));
#203217=CARTESIAN_POINT('Ctrl Pts',(-19.9339480823981,20.9550795883405,
19.0103139678715));
#203218=CARTESIAN_POINT('Ctrl Pts',(-19.9338620030314,20.9551388088677,
19.0103202055999));
#203219=CARTESIAN_POINT('Ctrl Pts',(-19.9336841343563,20.9552611588247,
19.0103330946722));
#203220=CARTESIAN_POINT('Ctrl Pts',(-19.9335923444732,20.9553242873652,
19.0103397460475));
#203221=CARTESIAN_POINT('Ctrl Pts',(-19.9334024105831,20.9554548924156,
19.0103535090615));
#203222=CARTESIAN_POINT('Ctrl Pts',(-19.9333042659174,20.9555223678525,
19.0103606207358));
#203223=CARTESIAN_POINT('Ctrl Pts',(-19.928070984362,20.9591196507895,19.0107398251101));
#203224=CARTESIAN_POINT('Ctrl Pts',(-19.9229203365489,20.9626267471199,
19.0111127765554));
#203225=CARTESIAN_POINT('Ctrl Pts',(-19.9111823831209,20.9705435415101,
19.0119621437524));
#203226=CARTESIAN_POINT('Ctrl Pts',(-19.9045856707945,20.9749390642151,
19.0124390877911));
#203227=CARTESIAN_POINT('Ctrl Pts',(-19.8856079655805,20.9874309534452,
19.0138101307927));
#203228=CARTESIAN_POINT('Ctrl Pts',(-19.8731667749699,20.9954346107718,
19.0147076757062));
#203229=CARTESIAN_POINT('Ctrl Pts',(-19.7870665135087,21.0495571748562,
19.0209116588197));
#203230=CARTESIAN_POINT('Ctrl Pts',(-19.7107213885186,21.0912269970739,
19.0263802955044));
#203231=CARTESIAN_POINT('Ctrl Pts',(-19.5002142292279,21.1898370772005,
19.041362164052));
#203232=CARTESIAN_POINT('Ctrl Pts',(-19.3623745568207,21.2378250907786,
19.0510971074492));
#203233=CARTESIAN_POINT('Ctrl Pts',(-19.1686221922198,21.2835970023539,
19.064123768228));
#203234=CARTESIAN_POINT('Ctrl Pts',(-19.1160714135176,21.2939251062326,
19.0675892319824));
#203235=CARTESIAN_POINT('Ctrl Pts',(-19.0356443044213,21.3065850847056,
19.0727392354969));
#203236=CARTESIAN_POINT('Ctrl Pts',(-19.0080217517752,21.3103757136771,
19.0744806576681));
#203237=CARTESIAN_POINT('Ctrl Pts',(-18.9734827023116,21.3144221109289,
19.076617480215));
#203238=CARTESIAN_POINT('Ctrl Pts',(-18.9666305192715,21.3151909575839,
19.0770394140795));
#203239=CARTESIAN_POINT('Ctrl Pts',(-18.9557640864944,21.3163564921782,
19.0777052490511));
#203240=CARTESIAN_POINT('Ctrl Pts',(-18.9517523188098,21.3167752010832,
19.0779503596852));
#203241=CARTESIAN_POINT('Ctrl Pts',(-18.9441719577815,21.3175444703217,
19.0784121347089));
#203242=CARTESIAN_POINT('Ctrl Pts',(-18.9406037151162,21.3178974256834,
19.0786289257584));
#203243=CARTESIAN_POINT('Ctrl Pts',(-18.9324281491159,21.3186851485056,
19.0791243394291));
#203244=CARTESIAN_POINT('Ctrl Pts',(-18.9278202899357,21.3191138754187,
19.0794026200616));
#203245=CARTESIAN_POINT('Ctrl Pts',(-18.9155512871331,21.3202148477527,
19.0801411602876));
#203246=CARTESIAN_POINT('Ctrl Pts',(-18.9078877422194,21.3208604695593,
19.0805999654418));
#203247=CARTESIAN_POINT('Ctrl Pts',(-18.8532924827852,21.3251604063639,
19.0838517383281));
#203248=CARTESIAN_POINT('Ctrl Pts',(-18.806250099316,21.3272905208898,19.0865655601787));
#203249=CARTESIAN_POINT('Ctrl Pts',(-18.723838485101,21.3282705044033,19.0912259481555));
#203250=CARTESIAN_POINT('Ctrl Pts',(-18.6884984494264,21.3278059531367,
19.0931942599116));
#203251=CARTESIAN_POINT('Ctrl Pts',(-18.5088934341252,21.3209446859869,
19.1031148531432));
#203252=CARTESIAN_POINT('Ctrl Pts',(-18.3655446402525,21.3006846503446,
19.1107882244793));
#203253=CARTESIAN_POINT('Ctrl Pts',(-18.1498061241505,21.2472874048348,
19.1231297656917));
#203254=CARTESIAN_POINT('Ctrl Pts',(-18.0753373027004,21.224432506524,19.1275372810849));
#203255=CARTESIAN_POINT('Ctrl Pts',(-17.9842993655213,21.1909004968648,
19.1331997171494));
#203256=CARTESIAN_POINT('Ctrl Pts',(-17.9663892477625,21.1840257768368,
19.1343271466788));
#203257=CARTESIAN_POINT('Ctrl Pts',(-17.9405677842116,21.1737095243329,
19.1359731727588));
#203258=CARTESIAN_POINT('Ctrl Pts',(-17.9325798270281,21.1704614211452,
19.1364852593386));
#203259=CARTESIAN_POINT('Ctrl Pts',(-17.9186427371285,21.1646947731278,
19.1373838757599));
#203260=CARTESIAN_POINT('Ctrl Pts',(-17.9126848365619,21.1621976151952,
19.1377696765811));
#203261=CARTESIAN_POINT('Ctrl Pts',(-17.9011622136924,21.1573059679266,
19.1385190707323));
#203262=CARTESIAN_POINT('Ctrl Pts',(-17.8955961505203,21.154914782875,19.1388825484548));
#203263=CARTESIAN_POINT('Ctrl Pts',(-17.8823527276467,21.1491579380113,
19.1397509439929));
#203264=CARTESIAN_POINT('Ctrl Pts',(-17.8746849880861,21.1457705229098,
19.1402566027372));
#203265=CARTESIAN_POINT('Ctrl Pts',(-17.8473048028855,21.1334797724892,
19.1420726525973));
#203266=CARTESIAN_POINT('Ctrl Pts',(-17.8277094675391,21.1243202200647,
19.1433918191923));
#203267=CARTESIAN_POINT('Ctrl Pts',(-17.6373490279054,21.0317586070133,
19.1564028942634));
#203268=CARTESIAN_POINT('Ctrl Pts',(-17.4784384557029,20.9260337740172,
19.1689388675631));
#203269=CARTESIAN_POINT('Ctrl Pts',(-17.2777781476593,20.749531281651,19.1865741499127));
#203270=CARTESIAN_POINT('Ctrl Pts',(-17.2225886338018,20.6953510003441,
19.1916444691733));
#203271=CARTESIAN_POINT('Ctrl Pts',(-17.1467200222394,20.6122399955117,
19.1988129755024));
#203272=CARTESIAN_POINT('Ctrl Pts',(-17.1236097314221,20.5856180460662,
19.2010261829913));
#203273=CARTESIAN_POINT('Ctrl Pts',(-17.0964520410258,20.5527081317394,
19.2036509814267));
#203274=CARTESIAN_POINT('Ctrl Pts',(-17.0917605665561,20.5469617044302,
19.2041053149122));
#203275=CARTESIAN_POINT('Ctrl Pts',(-17.0844924704814,20.5379631202775,
19.2048104280743));
#203276=CARTESIAN_POINT('Ctrl Pts',(-17.0818950929783,20.5347279136561,
19.205062665289));
#203277=CARTESIAN_POINT('Ctrl Pts',(-17.0770823192423,20.52869705257,19.2055304832227));
#203278=CARTESIAN_POINT('Ctrl Pts',(-17.0748644996438,20.5259034621915,
19.2057462338662));
#203279=CARTESIAN_POINT('Ctrl Pts',(-17.0698492653394,20.5195533256198,
19.2062345220013));
#203280=CARTESIAN_POINT('Ctrl Pts',(-17.0670561928381,20.5159934169565,
19.2065067493486));
#203281=CARTESIAN_POINT('Ctrl Pts',(-17.0587944816236,20.5053936555235,
19.2073129382117));
#203282=CARTESIAN_POINT('Ctrl Pts',(-17.0533587918804,20.498328085664,19.2078446192109));
#203283=CARTESIAN_POINT('Ctrl Pts',(-17.0125863679976,20.4446317077314,
19.2118440752282));
#203284=CARTESIAN_POINT('Ctrl Pts',(-16.9791483487723,20.3965838531807,
19.2151896658664));
#203285=CARTESIAN_POINT('Ctrl Pts',(-16.9338102353811,20.325306755169,19.2199207081904));
#203286=CARTESIAN_POINT('Ctrl Pts',(-16.9202828959771,20.3031506611426,
19.2213605209325));
#203287=CARTESIAN_POINT('Ctrl Pts',(-16.8894949372539,20.2505734796657,
19.2247185505662));
#203288=CARTESIAN_POINT('Ctrl Pts',(-16.8725738817601,20.2199622610429,
19.226628795461));
#203289=CARTESIAN_POINT('Ctrl Pts',(-16.8059466662384,20.0920430349865,
19.2344809016797));
#203290=CARTESIAN_POINT('Ctrl Pts',(-16.7630527418978,19.9913797145756,
19.2403645402569));
#203291=CARTESIAN_POINT('Ctrl Pts',(-16.7105361226236,19.8357463335977,
19.2494985279907));
#203292=CARTESIAN_POINT('Ctrl Pts',(-16.6949896865018,19.7829705794275,
19.2526001135353));
#203293=CARTESIAN_POINT('Ctrl Pts',(-16.6731233521427,19.6964380022404,
19.2577351816077));
#203294=CARTESIAN_POINT('Ctrl Pts',(-16.6655381810007,19.663026679826,19.2597294558342));
#203295=CARTESIAN_POINT('Ctrl Pts',(-16.6566319193872,19.6188572875588,
19.2623868581051));
#203296=CARTESIAN_POINT('Ctrl Pts',(-16.6545776757776,19.6082511804153,
19.2630265310129));
#203297=CARTESIAN_POINT('Ctrl Pts',(-16.6513451368779,19.5908490340386,
19.2640788291151));
#203298=CARTESIAN_POINT('Ctrl Pts',(-16.6501187007899,19.5840620546476,
19.2644899153744));
#203299=CARTESIAN_POINT('Ctrl Pts',(-16.6478082567528,19.5709093047483,
19.2652879421731));
#203300=CARTESIAN_POINT('Ctrl Pts',(-16.6467201653675,19.5645443221721,
19.2656747478645));
#203301=CARTESIAN_POINT('Ctrl Pts',(-16.644274193639,19.5498312099219,19.2665703468044));
#203302=CARTESIAN_POINT('Ctrl Pts',(-16.6429371943768,19.5414797638049,
19.2670797971981));
#203303=CARTESIAN_POINT('Ctrl Pts',(-16.6394743233533,19.5189865216858,
19.2684549500153));
#203304=CARTESIAN_POINT('Ctrl Pts',(-16.6374416711351,19.5048310153593,
19.2693235861058));
#203305=CARTESIAN_POINT('Ctrl Pts',(-16.6200053137569,19.3739944049202,
19.2773832049));
#203306=CARTESIAN_POINT('Ctrl Pts',(-16.614215954678,19.2562586098793,19.2848805640885));
#203307=CARTESIAN_POINT('Ctrl Pts',(-16.623825124451,18.9751838202362,19.3032565838769));
#203308=CARTESIAN_POINT('Ctrl Pts',(-16.6483428164416,18.8129023375953,
19.3142741634878));
#203309=CARTESIAN_POINT('Ctrl Pts',(-16.699437533551,18.6251631820092,19.3266195441605));
#203310=CARTESIAN_POINT('Ctrl Pts',(-16.7082309720774,18.595443920189,19.3285596068383));
#203311=CARTESIAN_POINT('Ctrl Pts',(-16.7198477210385,18.559133085433,19.3309034076885));
#203312=CARTESIAN_POINT('Ctrl Pts',(-16.7220555274467,18.552350381573,19.3313400661016));
#203313=CARTESIAN_POINT('Ctrl Pts',(-16.7255819785141,18.5416998075673,
19.3320237699227));
#203314=CARTESIAN_POINT('Ctrl Pts',(-16.7268775887796,18.5378244481199,
19.3322721351946));
#203315=CARTESIAN_POINT('Ctrl Pts',(-16.7293279256252,18.5305650960337,
19.3327365730172));
#203316=CARTESIAN_POINT('Ctrl Pts',(-16.7304799912676,18.5271803167993,
19.3329527922301));
#203317=CARTESIAN_POINT('Ctrl Pts',(-16.733139611945,18.5194307476886,19.3334470912534));
#203318=CARTESIAN_POINT('Ctrl Pts',(-16.7346528737838,18.5150679680834,
19.3337248296645));
#203319=CARTESIAN_POINT('Ctrl Pts',(-16.7393843956434,18.5015696620112,
19.3345825786688));
#203320=CARTESIAN_POINT('Ctrl Pts',(-16.7426511368823,18.4924510962974,
19.3351597918934));
#203321=CARTESIAN_POINT('Ctrl Pts',(-16.782233407973,18.3843072369727,19.3419824613633));
#203322=CARTESIAN_POINT('Ctrl Pts',(-16.825843217814,18.288092902431,19.347826747512));
#203323=CARTESIAN_POINT('Ctrl Pts',(-16.8828238724875,18.1838619972237,
19.3543153306785));
#203324=CARTESIAN_POINT('Ctrl Pts',(-16.8893067805204,18.1722640078486,
19.3550395624094));
#203325=CARTESIAN_POINT('Ctrl Pts',(-16.9500458701202,18.0659633657181,
19.3617043523912));
#203326=CARTESIAN_POINT('Ctrl Pts',(-17.0114401382486,17.9755293015901,
19.367582333004));
#203327=CARTESIAN_POINT('Ctrl Pts',(-17.1265553838227,17.8313289783191,
19.3778440205913));
#203328=CARTESIAN_POINT('Ctrl Pts',(-17.1766884818254,17.7749813951203,
19.3821175480254));
#203329=CARTESIAN_POINT('Ctrl Pts',(-17.2429809863635,17.7080340220333,
19.3876184696232));
#203330=CARTESIAN_POINT('Ctrl Pts',(-17.2564243099218,17.6948158172497,
19.3887267200522));
#203331=CARTESIAN_POINT('Ctrl Pts',(-17.2762273314517,17.6758579329323,
19.3903497715966));
#203332=CARTESIAN_POINT('Ctrl Pts',(-17.282448394039,17.6699742860051,19.3908583184327));
#203333=CARTESIAN_POINT('Ctrl Pts',(-17.2934182847214,17.6597247402399,
19.3917528344675));
#203334=CARTESIAN_POINT('Ctrl Pts',(-17.2981517212091,17.655342477018,19.3921380949773));
#203335=CARTESIAN_POINT('Ctrl Pts',(-17.3073819409107,17.6468750617717,
19.3928880058906));
#203336=CARTESIAN_POINT('Ctrl Pts',(-17.3118764307328,17.6427874948064,
19.3932525480644));
#203337=CARTESIAN_POINT('Ctrl Pts',(-17.3226630549573,17.6330619769255,
19.3941260119258));
#203338=CARTESIAN_POINT('Ctrl Pts',(-17.3289714303737,17.6274422674233,
19.3946356944235));
#203339=CARTESIAN_POINT('Ctrl Pts',(-17.3518580106305,17.6072985618245,
19.3964808122856));
#203340=CARTESIAN_POINT('Ctrl Pts',(-17.3686287026021,17.5929963089691,
19.3978253935882));
#203341=CARTESIAN_POINT('Ctrl Pts',(-17.5292457002971,17.4602956773197,
19.4106372794999));
#203342=CARTESIAN_POINT('Ctrl Pts',(-17.6878828996533,17.3611325344479,
19.4229109461565));
#203343=CARTESIAN_POINT('Ctrl Pts',(-17.9299281455313,17.2510237596132,
19.4404658321746));
#203344=CARTESIAN_POINT('Ctrl Pts',(-18.0042692086399,17.2221477973117,
19.4457001127579));
#203345=CARTESIAN_POINT('Ctrl Pts',(-18.1142142211104,17.1864398711878,
19.4530682522978));
#203346=CARTESIAN_POINT('Ctrl Pts',(-18.1486417971045,17.1762188678025,
19.455323835402));
#203347=CARTESIAN_POINT('Ctrl Pts',(-18.1905168607368,17.1649377553637,
19.4579918904362));
#203348=CARTESIAN_POINT('Ctrl Pts',(-18.1977290814757,17.1630356113103,
19.4584487351114));
#203349=CARTESIAN_POINT('Ctrl Pts',(-18.2089770486817,17.1601325770354,
19.4591568860153));
#203350=CARTESIAN_POINT('Ctrl Pts',(-18.2130058626501,17.1591054131555,
19.4594096698069));
#203351=CARTESIAN_POINT('Ctrl Pts',(-18.2204957745019,17.1572193089659,
19.4598779810289));
#203352=CARTESIAN_POINT('Ctrl Pts',(-18.2239559835913,17.1563572529343,
19.4600936816281));
#203353=CARTESIAN_POINT('Ctrl Pts',(-18.2317999597048,17.1544240876331,
19.4605811946995));
#203354=CARTESIAN_POINT('Ctrl Pts',(-18.2361849719355,17.1533582521489,
19.4608527011257));
#203355=CARTESIAN_POINT('Ctrl Pts',(-18.2475195531728,17.1506415856584,
19.4615519300798));
#203356=CARTESIAN_POINT('Ctrl Pts',(-18.2544741939716,17.149011875563,19.4619784668367));
#203357=CARTESIAN_POINT('Ctrl Pts',(-18.2973128436093,17.1392017725516,
19.4645912322538));
#203358=CARTESIAN_POINT('Ctrl Pts',(-18.3333992389099,17.1319225686439,
19.4667293464963));
#203359=CARTESIAN_POINT('Ctrl Pts',(-18.5372545400412,17.0963071907067,
19.4785490410011));
#203360=CARTESIAN_POINT('Ctrl Pts',(-18.7077828051435,17.0873335752921,
19.4875021820234));
#203361=CARTESIAN_POINT('Ctrl Pts',(-18.9729221913493,17.1053549287741,
19.5021193022167));
#203362=CARTESIAN_POINT('Ctrl Pts',(-19.0677256280792,17.1182866662317,
19.5074779677641));
#203363=CARTESIAN_POINT('Ctrl Pts',(-19.1822978235601,17.1418995625317,
19.5142895534746));
#203364=CARTESIAN_POINT('Ctrl Pts',(-19.2032036328508,17.1465399106918,
19.5155460470912));
#203365=CARTESIAN_POINT('Ctrl Pts',(-19.2328036959159,17.1535829013516,
19.5173458569852));
#203366=CARTESIAN_POINT('Ctrl Pts',(-19.2415589656451,17.1557252890582,
19.5178808110472));
#203367=CARTESIAN_POINT('Ctrl Pts',(-19.2566302080594,17.1595153500928,
19.5188062641754));
#203368=CARTESIAN_POINT('Ctrl Pts',(-19.2629527797747,17.1611364536929,
19.5191959006996));
#203369=CARTESIAN_POINT('Ctrl Pts',(-19.2750379683482,17.1642947240077,
19.5199433829838));
#203370=CARTESIAN_POINT('Ctrl Pts',(-19.2808017926091,17.1658270565946,
19.5203010687652));
#203371=CARTESIAN_POINT('Ctrl Pts',(-19.295759345937,17.1698713241267,19.5212324140364));
#203372=CARTESIAN_POINT('Ctrl Pts',(-19.3049426485793,17.1724210043251,
19.5218072952429));
#203373=CARTESIAN_POINT('Ctrl Pts',(-19.3361289682145,17.1813069240238,
19.5237702343509));
#203374=CARTESIAN_POINT('Ctrl Pts',(-19.3580456744929,17.1879379128245,
19.5251678515803));
#203375=CARTESIAN_POINT('Ctrl Pts',(-19.548203047858,17.2488547856926,19.537457156646));
#203376=CARTESIAN_POINT('Ctrl Pts',(-19.7091077895023,17.3236523101553,
19.5490643047287));
#203377=CARTESIAN_POINT('Ctrl Pts',(-19.9317637694991,17.4632969362629,
19.5664282131301));
#203378=CARTESIAN_POINT('Ctrl Pts',(-20.0018593303351,17.5134609994542,
19.5721011973772));
#203379=CARTESIAN_POINT('Ctrl Pts',(-20.097888861105,17.5914601044017,19.579998338313));
#203380=CARTESIAN_POINT('Ctrl Pts',(-20.1264353098609,17.6159368006453,
19.5823627329963));
#203381=CARTESIAN_POINT('Ctrl Pts',(-20.159921597287,17.6462336497171,19.5851414786787));
#203382=CARTESIAN_POINT('Ctrl Pts',(-20.1654994975822,17.6513348676824,
19.585604517822));
#203383=CARTESIAN_POINT('Ctrl Pts',(-20.1741190256151,17.6593029743435,
19.5863201575645));
#203384=CARTESIAN_POINT('Ctrl Pts',(-20.1771796217529,17.6621491203399,
19.5865742856182));
#203385=CARTESIAN_POINT('Ctrl Pts',(-20.1828344831225,17.6674390707224,
19.587043825551));
#203386=CARTESIAN_POINT('Ctrl Pts',(-20.1854309831364,17.6698803409972,
19.5872594185393));
#203387=CARTESIAN_POINT('Ctrl Pts',(-20.191280159151,17.6754077231099,19.5877450956895));
#203388=CARTESIAN_POINT('Ctrl Pts',(-20.1945291941452,17.6784976094637,
19.5880148835894));
#203389=CARTESIAN_POINT('Ctrl Pts',(-20.2040697214724,17.6876287084534,
19.5888072098692));
#203390=CARTESIAN_POINT('Ctrl Pts',(-20.2103338113511,17.6936985924732,
19.5893275825398));
#203391=CARTESIAN_POINT('Ctrl Pts',(-20.2546653754833,17.7371902075102,
19.5930129526955));
#203392=CARTESIAN_POINT('Ctrl Pts',(-20.2913463584163,17.7760045888628,
19.5960764366407));
#203393=CARTESIAN_POINT('Ctrl Pts',(-20.3355351790522,17.8264563437825,
19.5998480552725));
#203394=CARTESIAN_POINT('Ctrl Pts',(-20.3444469243096,17.83683233148,19.6006131013246));
#203395=CARTESIAN_POINT('Ctrl Pts',(-20.3868878945445,17.8872265294452,
19.6042819091224));
#203396=CARTESIAN_POINT('Ctrl Pts',(-20.41903072729,17.928390774779,19.6071384787977));
#203397=CARTESIAN_POINT('Ctrl Pts',(-20.5137301712,18.0593821262715,19.6159391053306));
#203398=CARTESIAN_POINT('Ctrl Pts',(-20.5708676845734,18.1528981882664,
19.6218309622777));
#203399=CARTESIAN_POINT('Ctrl Pts',(-20.6549212173413,18.3179719316179,
19.6321302759991));
#203400=CARTESIAN_POINT('Ctrl Pts',(-20.6856664510528,18.3873290901251,
19.6364279098019));
#203401=CARTESIAN_POINT('Ctrl Pts',(-20.7193494083111,18.4758575524414,
19.6419578861143));
#203402=CARTESIAN_POINT('Ctrl Pts',(-20.7258375509708,18.493622953052,19.6430696069066));
#203403=CARTESIAN_POINT('Ctrl Pts',(-20.7349196687835,18.5195645463489,
19.6446968180629));
#203404=CARTESIAN_POINT('Ctrl Pts',(-20.7377034727636,18.527673652325,19.6452060082569));
#203405=CARTESIAN_POINT('Ctrl Pts',(-20.7424958165883,18.541914664089,19.6461012683676));
#203406=CARTESIAN_POINT('Ctrl Pts',(-20.7445257362882,18.5480392965761,
19.6464866259066));
#203407=CARTESIAN_POINT('Ctrl Pts',(-20.7484115459096,18.5599454756364,
19.6472364380232));
#203408=CARTESIAN_POINT('Ctrl Pts',(-20.7502706246648,18.5657259210947,
19.6476007830185));
#203409=CARTESIAN_POINT('Ctrl Pts',(-20.7546531727144,18.5795564733271,
19.6484733100267));
#203410=CARTESIAN_POINT('Ctrl Pts',(-20.7571534260446,18.5876137768294,
19.6489822491658));
#203411=CARTESIAN_POINT('Ctrl Pts',(-20.7659891994505,18.6167010109599,
19.6508219303307));
#203412=CARTESIAN_POINT('Ctrl Pts',(-20.772045345411,18.6378137230619,19.6521617482522));
#203413=CARTESIAN_POINT('Ctrl Pts',(-20.8265422866381,18.8395937663336,
19.6650135735315));
#203414=CARTESIAN_POINT('Ctrl Pts',(-20.8511563470631,19.0258066908902,
19.6773393374397));
#203415=CARTESIAN_POINT('Ctrl Pts',(-20.850946310095,19.2757905616587,19.6938413459655));
#203416=CARTESIAN_POINT('Ctrl Pts',(-20.8480800912412,19.3387716790032,
19.6979838416257));
#203417=CARTESIAN_POINT('Ctrl Pts',(-20.8379188606408,19.4512138802063,
19.7052635903443));
#203418=CARTESIAN_POINT('Ctrl Pts',(-20.8316744049217,19.5007244175735,
19.7084279455097));
#203419=CARTESIAN_POINT('Ctrl Pts',(-20.8224344769448,19.5576864775276,
19.7119866950838));
#203420=CARTESIAN_POINT('Ctrl Pts',(-20.8211403746751,19.5653940446792,
19.7124664790857));
#203421=CARTESIAN_POINT('Ctrl Pts',(-20.8190058160902,19.5776899264423,
19.7132288856703));
#203422=CARTESIAN_POINT('Ctrl Pts',(-20.8181928415456,19.5822828510634,
19.7135130019263));
#203423=CARTESIAN_POINT('Ctrl Pts',(-20.8167271896715,19.5904065697911,
19.7140143026017));
#203424=CARTESIAN_POINT('Ctrl Pts',(-20.8160807012237,19.5939384364748,
19.7142318347685));
#203425=CARTESIAN_POINT('Ctrl Pts',(-20.8146926430744,19.6014141754152,
19.7146913854627));
#203426=CARTESIAN_POINT('Ctrl Pts',(-20.8139488460453,19.6053575810862,
19.7149332755635));
#203427=CARTESIAN_POINT('Ctrl Pts',(-20.8119140362788,19.6159796643295,
19.7155834940726));
#203428=CARTESIAN_POINT('Ctrl Pts',(-20.8106020269407,19.6226543395387,
19.7159906425494));
#203429=CARTESIAN_POINT('Ctrl Pts',(-20.8039707292014,19.6555515583572,
19.7179907747884));
#203430=CARTESIAN_POINT('Ctrl Pts',(-20.7981865499891,19.6816792383203,
19.7195587194152));
#203431=CARTESIAN_POINT('Ctrl Pts',(-20.7800922296375,19.7566481994357,
19.7240163436332));
#203432=CARTESIAN_POINT('Ctrl Pts',(-20.7665321440998,19.8051709596792,
19.7268506308771));
#203433=CARTESIAN_POINT('Ctrl Pts',(-20.7422796869634,19.8813557567109,
19.7312843855716));
#203434=CARTESIAN_POINT('Ctrl Pts',(-20.7327195890317,19.9093429217765,
19.7329095481473));
#203435=CARTESIAN_POINT('Ctrl Pts',(-20.7225805741668,19.9371103910883,
19.7345261348292));
#203436=CARTESIAN_POINT('Origin',(-18.734,19.211,0.));
#203437=CARTESIAN_POINT('',(-20.7225806115196,19.937110288791,20.7554137119617));
#203438=CARTESIAN_POINT('',(-20.7225806064498,19.9371103026755,20.5336910513061));
#203439=CARTESIAN_POINT('',(-20.7225806064498,19.9371103026755,0.));
#203440=CARTESIAN_POINT('Ctrl Pts',(-20.7225806115197,19.937110288791,20.7554137119617));
#203441=CARTESIAN_POINT('Ctrl Pts',(-20.7319594608855,19.9114246618344,
20.7536067965805));
#203442=CARTESIAN_POINT('Ctrl Pts',(-20.7408447670006,19.8855460679731,
20.7517981735461));
#203443=CARTESIAN_POINT('Ctrl Pts',(-20.7725200156157,19.7871126712942,
20.744976017502));
#203444=CARTESIAN_POINT('Ctrl Pts',(-20.791895809394,19.7135296827932,20.7399903788199));
#203445=CARTESIAN_POINT('Ctrl Pts',(-20.8143280456744,19.6048809225687,
20.7329254081469));
#203446=CARTESIAN_POINT('Ctrl Pts',(-20.8205389580097,19.5705308933176,
20.730734451597));
#203447=CARTESIAN_POINT('Ctrl Pts',(-20.8270336482829,19.528732356022,20.7281324246831));
#203448=CARTESIAN_POINT('Ctrl Pts',(-20.8281309514486,19.5214178873819,
20.7276794520147));
#203449=CARTESIAN_POINT('Ctrl Pts',(-20.8297832003997,19.5099965687853,
20.7269759956358));
#203450=CARTESIAN_POINT('Ctrl Pts',(-20.8303644473521,19.5058936686014,
20.72672406501));
#203451=CARTESIAN_POINT('Ctrl Pts',(-20.831423622601,19.4982557598256,20.7262565460339));
#203452=CARTESIAN_POINT('Ctrl Pts',(-20.8319046586589,19.4947212851344,
20.7260407894414));
#203453=CARTESIAN_POINT('Ctrl Pts',(-20.8329764095951,19.4866946847737,
20.7255521419681));
#203454=CARTESIAN_POINT('Ctrl Pts',(-20.8335616373001,19.4822018792406,
20.7252795633578));
#203455=CARTESIAN_POINT('Ctrl Pts',(-20.8352591881885,19.4688348537539,
20.7244712782587));
#203456=CARTESIAN_POINT('Ctrl Pts',(-20.8363297205133,19.4599552979474,
20.7239378705038));
#203457=CARTESIAN_POINT('Ctrl Pts',(-20.84407733881,19.3920752179413,20.7198853164858));
#203458=CARTESIAN_POINT('Ctrl Pts',(-20.8483264321573,19.332818346711,20.7164920697119));
#203459=CARTESIAN_POINT('Ctrl Pts',(-20.8506770362225,19.2531771322551,
20.7120328020572));
#203460=CARTESIAN_POINT('Ctrl Pts',(-20.8509840406739,19.2328904078398,
20.7109057277409));
#203461=CARTESIAN_POINT('Ctrl Pts',(-20.8511051845657,19.0728052824201,
20.7020608117506));
#203462=CARTESIAN_POINT('Ctrl Pts',(-20.8373639114502,18.9333413712754,
20.6946257510641));
#203463=CARTESIAN_POINT('Ctrl Pts',(-20.7922497953957,18.7075304791036,
20.6818795084201));
#203464=CARTESIAN_POINT('Ctrl Pts',(-20.7688588121515,18.6200511751906,
20.6767638173073));
#203465=CARTESIAN_POINT('Ctrl Pts',(-20.7355595959724,18.5213358782081,
20.670656054497));
#203466=CARTESIAN_POINT('Ctrl Pts',(-20.731045868669,18.5083726433531,20.6698472828421));
#203467=CARTESIAN_POINT('Ctrl Pts',(-20.7236045524634,18.4876526117024,
20.6685433909434));
#203468=CARTESIAN_POINT('Ctrl Pts',(-20.7207568610039,18.4798673912279,
20.6680509247335));
#203469=CARTESIAN_POINT('Ctrl Pts',(-20.7156191778919,18.4660733041462,
20.6671737389019));
#203470=CARTESIAN_POINT('Ctrl Pts',(-20.7133473834866,18.4600577369328,
20.6667896316463));
#203471=CARTESIAN_POINT('Ctrl Pts',(-20.7085566166868,18.4475448755953,
20.6659873429947));
#203472=CARTESIAN_POINT('Ctrl Pts',(-20.7060329030993,18.4410494907019,
20.665569005995));
#203473=CARTESIAN_POINT('Ctrl Pts',(-20.6993949387511,18.4242118304519,
20.6644796438639));
#203474=CARTESIAN_POINT('Ctrl Pts',(-20.6952311498232,18.4138894314087,
20.6638069544908));
#203475=CARTESIAN_POINT('Ctrl Pts',(-20.6767885690955,18.3691880460115,
20.6608723820402));
#203476=CARTESIAN_POINT('Ctrl Pts',(-20.6616864794048,18.3351579187671,
20.6585827206034));
#203477=CARTESIAN_POINT('Ctrl Pts',(-20.6191743051355,18.2457963052023,
20.6524167207909));
#203478=CARTESIAN_POINT('Ctrl Pts',(-20.5902290418303,18.1912387775485,
20.6484906099546));
#203479=CARTESIAN_POINT('Ctrl Pts',(-20.4847193340871,18.0117847032291,
20.6350415632723));
#203480=CARTESIAN_POINT('Ctrl Pts',(-20.3975967056339,17.8935872679175,
20.6252363275487));
#203481=CARTESIAN_POINT('Ctrl Pts',(-20.2858389487258,17.7709076254773,
20.6144037567855));
#203482=CARTESIAN_POINT('Ctrl Pts',(-20.2724917961671,17.7566571257403,
20.6131348661711));
#203483=CARTESIAN_POINT('Ctrl Pts',(-20.2223172484832,17.7045505680223,
20.6084614050712));
#203484=CARTESIAN_POINT('Ctrl Pts',(-20.1842711531,17.6678886251204,20.605105231731));
#203485=CARTESIAN_POINT('Ctrl Pts',(-20.1384093794248,17.6268917773531,
20.601310736214));
#203486=CARTESIAN_POINT('Ctrl Pts',(-20.1318927161191,17.6211382053026,
20.6007772142511));
#203487=CARTESIAN_POINT('Ctrl Pts',(-20.1219663903597,17.6124824547285,
20.5999733084864));
#203488=CARTESIAN_POINT('Ctrl Pts',(-20.1185827491749,17.6095507641988,
20.5997008031928));
#203489=CARTESIAN_POINT('Ctrl Pts',(-20.1124893426092,17.6043049979951,
20.5992128389033));
#203490=CARTESIAN_POINT('Ctrl Pts',(-20.1097830253459,17.6019870215254,
20.5989970938741));
#203491=CARTESIAN_POINT('Ctrl Pts',(-20.1038860824252,17.5969620114554,
20.5985291224611));
#203492=CARTESIAN_POINT('Ctrl Pts',(-20.1006932904125,17.5942576092882,
20.5982770887486));
#203493=CARTESIAN_POINT('Ctrl Pts',(-20.0916937737522,17.5866804261981,
20.5975703739912));
#203494=CARTESIAN_POINT('Ctrl Pts',(-20.0858687975873,17.5818292848294,
20.5971172488461));
#203495=CARTESIAN_POINT('Ctrl Pts',(-20.0507099894218,17.5528668276233,
20.5944070919613));
#203496=CARTESIAN_POINT('Ctrl Pts',(-20.0207558647556,17.5295153697371,
20.5922013954487));
#203497=CARTESIAN_POINT('Ctrl Pts',(-19.9196794697699,17.4550027540113,
20.5850329924155));
#203498=CARTESIAN_POINT('Ctrl Pts',(-19.8460072153081,17.4074466970137,
20.5802385721238));
#203499=CARTESIAN_POINT('Ctrl Pts',(-19.6172789241837,17.2791600141768,
20.5659713132993));
#203500=CARTESIAN_POINT('Ctrl Pts',(-19.4549969360529,17.2129148995996,
20.5565784041035));
#203501=CARTESIAN_POINT('Ctrl Pts',(-19.264170974169,17.1613318975066,20.5450925279135));
#203502=CARTESIAN_POINT('Ctrl Pts',(-19.2418174041197,17.1556795834021,
20.5437418189163));
#203503=CARTESIAN_POINT('Ctrl Pts',(-19.2100739715762,17.1482024059493,
20.5418145788387));
#203504=CARTESIAN_POINT('Ctrl Pts',(-19.2007567289617,17.146074216382,20.5412477970871));
#203505=CARTESIAN_POINT('Ctrl Pts',(-19.1855973918144,17.1427194517776,
20.5403237225324));
#203506=CARTESIAN_POINT('Ctrl Pts',(-19.1797638916359,17.1414543536712,
20.5399676695837));
#203507=CARTESIAN_POINT('Ctrl Pts',(-19.1675441579272,17.1388583499105,
20.5392208366072));
#203508=CARTESIAN_POINT('Ctrl Pts',(-19.1611569757308,17.1375322593504,
20.5388299066604));
#203509=CARTESIAN_POINT('Ctrl Pts',(-19.1459516440064,17.1344486061607,
20.5378978712834));
#203510=CARTESIAN_POINT('Ctrl Pts',(-19.137128278846,17.132717671934,20.5373559214713));
#203511=CARTESIAN_POINT('Ctrl Pts',(-19.1073848159145,17.1270792492144,
20.5355251447754));
#203512=CARTESIAN_POINT('Ctrl Pts',(-19.0864174187928,17.1234311203348,
20.5342281069482));
#203513=CARTESIAN_POINT('Ctrl Pts',(-18.9080248086676,17.0951566177093,
20.5231347158308));
#203514=CARTESIAN_POINT('Ctrl Pts',(-18.7483666254294,17.0880649382601,
20.5127652433662));
#203515=CARTESIAN_POINT('Ctrl Pts',(-18.458107873658,17.1079294302074,20.4935470591489));
#203516=CARTESIAN_POINT('Ctrl Pts',(-18.3278725959667,17.1291525195447,
20.4848055002219));
#203517=CARTESIAN_POINT('Ctrl Pts',(-18.1852097317475,17.1663078288577,
20.4756083763572));
#203518=CARTESIAN_POINT('Ctrl Pts',(-18.1700194199341,17.170445474349,20.4746342979864));
#203519=CARTESIAN_POINT('Ctrl Pts',(-18.1492987920717,17.1763385734168,
20.4733140610667));
#203520=CARTESIAN_POINT('Ctrl Pts',(-18.1437278747749,17.1779477519309,
20.4729599469653));
#203521=CARTESIAN_POINT('Ctrl Pts',(-18.1348886176375,17.1805403969771,
20.4723995005999));
#203522=CARTESIAN_POINT('Ctrl Pts',(-18.1316159712683,17.1815088986902,
20.4721923107605));
#203523=CARTESIAN_POINT('Ctrl Pts',(-18.1248643808252,17.183524723435,20.4717655314615));
#203524=CARTESIAN_POINT('Ctrl Pts',(-18.1213857891828,17.1845730882947,
20.4715460102469));
#203525=CARTESIAN_POINT('Ctrl Pts',(-18.1131073251393,17.1870912853772,
20.4710244270176));
#203526=CARTESIAN_POINT('Ctrl Pts',(-18.1083099118622,17.1885692561649,
20.470722839672));
#203527=CARTESIAN_POINT('Ctrl Pts',(-18.0921655793462,17.1936058909986,
20.4697100607117));
#203528=CARTESIAN_POINT('Ctrl Pts',(-18.0808431626198,17.1972431688565,
20.4690033218647));
#203529=CARTESIAN_POINT('Ctrl Pts',(-17.9457644037088,17.2418957899126,
20.4606076528749));
#203530=CARTESIAN_POINT('Ctrl Pts',(-17.8260028073034,17.2941698765269,
20.4535153747759));
#203531=CARTESIAN_POINT('Ctrl Pts',(-17.5697669395943,17.4354558547063,
20.4376192524189));
#203532=CARTESIAN_POINT('Ctrl Pts',(-17.4372220491727,17.529823152826,20.428839909868));
#203533=CARTESIAN_POINT('Ctrl Pts',(-17.2991276785097,17.6542747879464,
20.4180455186159));
#203534=CARTESIAN_POINT('Ctrl Pts',(-17.2817710489797,17.6704536774819,
20.4166561462275));
#203535=CARTESIAN_POINT('Ctrl Pts',(-17.2577300776008,17.6936307002352,
20.4146830950954));
#203536=CARTESIAN_POINT('Ctrl Pts',(-17.2508157880993,17.7003885130496,
20.4141098133899));
#203537=CARTESIAN_POINT('Ctrl Pts',(-17.2396937293743,17.7114088425107,
20.4131780377926));
#203538=CARTESIAN_POINT('Ctrl Pts',(-17.2354572831054,17.7156423188553,
20.4128208258322));
#203539=CARTESIAN_POINT('Ctrl Pts',(-17.2266562504412,17.7245121421823,
20.4120738932573));
#203540=CARTESIAN_POINT('Ctrl Pts',(-17.2220949648797,17.7291516629275,
20.4116840330172));
#203541=CARTESIAN_POINT('Ctrl Pts',(-17.2113470127608,17.7401852466036,
20.4107588038574));
#203542=CARTESIAN_POINT('Ctrl Pts',(-17.2051791613167,17.7465973921808,
20.4102226229608));
#203543=CARTESIAN_POINT('Ctrl Pts',(-17.1847745268702,17.7680796195697,
20.4084311588112));
#203544=CARTESIAN_POINT('Ctrl Pts',(-17.1707190562697,17.7833195617206,
20.4071681362666));
#203545=CARTESIAN_POINT('Ctrl Pts',(-17.0968871011185,17.8657711017735,
20.400374317518));
#203546=CARTESIAN_POINT('Ctrl Pts',(-17.0412232627048,17.9365264810432,
20.3946755832227));
#203547=CARTESIAN_POINT('Ctrl Pts',(-16.9134444272628,18.1221449757554,
20.380071654885));
#203548=CARTESIAN_POINT('Ctrl Pts',(-16.8475388060186,18.2407998440682,
20.3710207776676));
#203549=CARTESIAN_POINT('Ctrl Pts',(-16.7632408397996,18.4341472259182,
20.3572277647944));
#203550=CARTESIAN_POINT('Ctrl Pts',(-16.73678177814,18.5049449098675,20.3523662003512));
#203551=CARTESIAN_POINT('Ctrl Pts',(-16.7113184618252,18.5860692024997,
20.3471147443877));
#203552=CARTESIAN_POINT('Ctrl Pts',(-16.7085366015627,18.5951451990588,
20.3465316486341));
#203553=CARTESIAN_POINT('Ctrl Pts',(-16.7045031605297,18.6086275618938,
20.3456723275603));
#203554=CARTESIAN_POINT('Ctrl Pts',(-16.7032047245632,18.6130196275928,
20.3453934677242));
#203555=CARTESIAN_POINT('Ctrl Pts',(-16.7009190838297,18.6208443044117,
20.3448986220294));
#203556=CARTESIAN_POINT('Ctrl Pts',(-16.6999263046087,18.6242752271264,
20.3446823147866));
#203557=CARTESIAN_POINT('Ctrl Pts',(-16.6978096390765,18.6316601082382,
20.3442181733061));
#203558=CARTESIAN_POINT('Ctrl Pts',(-16.6966885873758,18.6356148205278,
20.3439705047833));
#203559=CARTESIAN_POINT('Ctrl Pts',(-16.6936238539204,18.6465474765274,
20.3432882160112));
#203560=CARTESIAN_POINT('Ctrl Pts',(-16.6917044350856,18.6535322451253,
20.3428549835999));
#203561=CARTESIAN_POINT('Ctrl Pts',(-16.6813527832255,18.6919730489355,
20.3404846691113));
#203562=CARTESIAN_POINT('Ctrl Pts',(-16.6736109104277,18.723612438899,20.3385851003717));
#203563=CARTESIAN_POINT('Ctrl Pts',(-16.6315987518309,18.9142613278309,
20.3273764793654));
#203564=CARTESIAN_POINT('Ctrl Pts',(-16.6150144513749,19.0766239483737,
20.3187792468002));
#203565=CARTESIAN_POINT('Ctrl Pts',(-16.6187508688498,19.3561207785592,
20.3034768593061));
#203566=CARTESIAN_POINT('Ctrl Pts',(-16.6299799881108,19.4725978897949,
20.2969546135077));
#203567=CARTESIAN_POINT('Ctrl Pts',(-16.6532984651167,19.6016076314741,
20.2892743280244));
#203568=CARTESIAN_POINT('Ctrl Pts',(-16.6559824261698,19.615643234189,20.2884328251108));
#203569=CARTESIAN_POINT('Ctrl Pts',(-16.6604801817901,19.6379379861606,
20.2870862559164));
#203570=CARTESIAN_POINT('Ctrl Pts',(-16.6622017498402,19.6462154501024,
20.2865841308636));
#203571=CARTESIAN_POINT('Ctrl Pts',(-16.6653254325329,19.6607957573312,
20.285695729946));
#203572=CARTESIAN_POINT('Ctrl Pts',(-16.6667068937379,19.667102949754,20.2853101201121));
#203573=CARTESIAN_POINT('Ctrl Pts',(-16.6696238752663,19.6801351604111,
20.2845106172281));
#203574=CARTESIAN_POINT('Ctrl Pts',(-16.6711634531293,19.6868591832116,
20.2840965978255));
#203575=CARTESIAN_POINT('Ctrl Pts',(-16.6751997194969,19.7040996174062,
20.2830311069467));
#203576=CARTESIAN_POINT('Ctrl Pts',(-16.677744112739,19.7146045541937,20.2823781060042));
#203577=CARTESIAN_POINT('Ctrl Pts',(-16.6886997911577,19.7583691662894,
20.2796415520354));
#203578=CARTESIAN_POINT('Ctrl Pts',(-16.6978380967502,19.7914398641706,
20.2775346565797));
#203579=CARTESIAN_POINT('Ctrl Pts',(-16.7237398566325,19.8770181068045,
20.2719769928336));
#203580=CARTESIAN_POINT('Ctrl Pts',(-16.7417565160111,19.9291163151129,
20.2684877832575));
#203581=CARTESIAN_POINT('Ctrl Pts',(-16.8015457833695,20.0823653990312,
20.25791417993));
#203582=CARTESIAN_POINT('Ctrl Pts',(-16.8491453204952,20.1810393442023,
20.2506814069109));
#203583=CARTESIAN_POINT('Ctrl Pts',(-16.9285020628891,20.317440726491,20.2402571474394));
#203584=CARTESIAN_POINT('Ctrl Pts',(-16.95428280989,20.3584497122096,20.2370647154989));
#203585=CARTESIAN_POINT('Ctrl Pts',(-16.9913672209158,20.4131783104903,
20.2327518680978));
#203586=CARTESIAN_POINT('Ctrl Pts',(-17.0014698655874,20.4276926690173,
20.2316028871623));
#203587=CARTESIAN_POINT('Ctrl Pts',(-17.0427745989141,20.4854768865867,
20.2270123268101));
#203588=CARTESIAN_POINT('Ctrl Pts',(-17.0754280444275,20.5276908507773,
20.2236211945346));
#203589=CARTESIAN_POINT('Ctrl Pts',(-17.1152364292531,20.575320174496,20.2197919623708));
#203590=CARTESIAN_POINT('Ctrl Pts',(-17.1208698812611,20.5819763902199,
20.2192567625324));
#203591=CARTESIAN_POINT('Ctrl Pts',(-17.1294617005198,20.5920017898809,
20.2184508166554));
#203592=CARTESIAN_POINT('Ctrl Pts',(-17.1323898274872,20.595396602969,20.2181779338012));
#203593=CARTESIAN_POINT('Ctrl Pts',(-17.137665022377,20.6014734231494,20.2176895557199));
#203594=CARTESIAN_POINT('Ctrl Pts',(-17.1400080879951,20.6041588158979,
20.2174737723777));
#203595=CARTESIAN_POINT('Ctrl Pts',(-17.1451139090325,20.609980864961,20.2170060241877));
#203596=CARTESIAN_POINT('Ctrl Pts',(-17.1478791669049,20.6131152499392,
20.216754250361));
#203597=CARTESIAN_POINT('Ctrl Pts',(-17.1556721850333,20.6218959802807,
20.2160489851467));
#203598=CARTESIAN_POINT('Ctrl Pts',(-17.1607209933318,20.6275236777955,
20.2155970395043));
#203599=CARTESIAN_POINT('Ctrl Pts',(-17.1910740434903,20.6609944899808,
20.2129086417882));
#203600=CARTESIAN_POINT('Ctrl Pts',(-17.2170884181499,20.6881879279899,
20.2107225725016));
#203601=CARTESIAN_POINT('Ctrl Pts',(-17.3050599681396,20.7753702031143,
20.2036497927681));
#203602=CARTESIAN_POINT('Ctrl Pts',(-17.3699603895679,20.8322717350403,
20.1989262911385));
#203603=CARTESIAN_POINT('Ctrl Pts',(-17.5778023360435,20.9931566253885,
20.1846226480845));
#203604=CARTESIAN_POINT('Ctrl Pts',(-17.730408020612,21.0833439234493,20.1751339207402));
#203605=CARTESIAN_POINT('Ctrl Pts',(-17.9134551616087,21.1626454603613,
20.1635410827757));
#203606=CARTESIAN_POINT('Ctrl Pts',(-17.9346222919178,21.1714104300638,
20.1621988566356));
#203607=CARTESIAN_POINT('Ctrl Pts',(-17.9647924607332,21.1833335506415,
20.1602816708539));
#203608=CARTESIAN_POINT('Ctrl Pts',(-17.9736814654442,21.1867772128821,
20.1597163216907));
#203609=CARTESIAN_POINT('Ctrl Pts',(-17.9881694342987,21.1922777044502,
20.1587939589089));
#203610=CARTESIAN_POINT('Ctrl Pts',(-17.9937544296414,21.1943711375659,
20.1584381760813));
#203611=CARTESIAN_POINT('Ctrl Pts',(-18.0054694057876,21.198705907113,20.1576914007266));
#203612=CARTESIAN_POINT('Ctrl Pts',(-18.0116010459482,21.2009425493163,
20.1573002560392));
#203613=CARTESIAN_POINT('Ctrl Pts',(-18.026223355109,21.2061998486978,20.1563667679629));
#203614=CARTESIAN_POINT('Ctrl Pts',(-18.0347231103111,21.2091946959489,
20.1558235730168));
#203615=CARTESIAN_POINT('Ctrl Pts',(-18.063474169852,21.2191190806929,20.1539841059794));
#203616=CARTESIAN_POINT('Ctrl Pts',(-18.0838108543454,21.2257955611465,
20.1526795157118));
#203617=CARTESIAN_POINT('Ctrl Pts',(-18.1954218305781,21.2605713934878,
20.1454985875525));
#203618=CARTESIAN_POINT('Ctrl Pts',(-18.2884045165872,21.2827745397511,
20.1394321265378));
#203619=CARTESIAN_POINT('Ctrl Pts',(-18.5505653488837,21.3269081264424,
20.1221547077014));
#203620=CARTESIAN_POINT('Ctrl Pts',(-18.7213619391097,21.3348061779101,
20.1106597896389));
#203621=CARTESIAN_POINT('Ctrl Pts',(-18.9278509626435,21.3194253804058,
20.097445229846));
#203622=CARTESIAN_POINT('Ctrl Pts',(-18.9643736387357,21.3157479995503,
20.0951369196735));
#203623=CARTESIAN_POINT('Ctrl Pts',(-19.0078641269271,21.3102232772998,
20.0924372735665));
#203624=CARTESIAN_POINT('Ctrl Pts',(-19.0149391402448,21.3092881429308,
20.091999656085));
#203625=CARTESIAN_POINT('Ctrl Pts',(-19.0264781434135,21.3077035751006,
20.0912886202263));
#203626=CARTESIAN_POINT('Ctrl Pts',(-19.0309449585705,21.3070756280881,
20.0910140347365));
#203627=CARTESIAN_POINT('Ctrl Pts',(-19.0389393201024,21.3059257090552,
20.0905238279934));
#203628=CARTESIAN_POINT('Ctrl Pts',(-19.0424675729542,21.3054090986354,
20.09030790914));
#203629=CARTESIAN_POINT('Ctrl Pts',(-19.0501083029149,21.3042706082124,
20.0898412565913));
#203630=CARTESIAN_POINT('Ctrl Pts',(-19.0542202447514,21.3036455251458,
20.0895907064297));
#203631=CARTESIAN_POINT('Ctrl Pts',(-19.0657076913509,21.3018645916607,
20.0888923157202));
#203632=CARTESIAN_POINT('Ctrl Pts',(-19.0730790475414,21.3006818266059,
20.0884459728507));
#203633=CARTESIAN_POINT('Ctrl Pts',(-19.1159749303773,21.2935660447723,
20.085858307056));
#203634=CARTESIAN_POINT('Ctrl Pts',(-19.1513519635593,21.2867658502693,
20.0837630738567));
#203635=CARTESIAN_POINT('Ctrl Pts',(-19.2647854184227,21.2619439916857,
20.0771209800265));
#203636=CARTESIAN_POINT('Ctrl Pts',(-19.3420019693395,21.2403940049983,
20.0727154284637));
#203637=CARTESIAN_POINT('Ctrl Pts',(-19.5935258045246,21.1545469261092,
20.0582269968559));
#203638=CARTESIAN_POINT('Ctrl Pts',(-19.76056264221,21.0717316821763,20.0482971339798));
#203639=CARTESIAN_POINT('Ctrl Pts',(-19.9329971413593,20.9558733814055,
20.0362146834589));
#203640=CARTESIAN_POINT('Ctrl Pts',(-19.9511436682172,20.9432639807019,
20.0349193587355));
#203641=CARTESIAN_POINT('Ctrl Pts',(-19.9759578324821,20.9254390536575,
20.0331133193342));
#203642=CARTESIAN_POINT('Ctrl Pts',(-19.9827969500325,20.9204638635564,
20.0326118280876));
#203643=CARTESIAN_POINT('Ctrl Pts',(-19.9944992178101,20.9118432200179,
20.0317472244393));
#203644=CARTESIAN_POINT('Ctrl Pts',(-19.9993768526169,20.9082175337466,
20.0313848825236));
#203645=CARTESIAN_POINT('Ctrl Pts',(-20.0092323688007,20.9008255440933,
20.0306487201526));
#203646=CARTESIAN_POINT('Ctrl Pts',(-20.0142093374333,20.8970581291763,
20.0302748583196));
#203647=CARTESIAN_POINT('Ctrl Pts',(-20.0257370299678,20.8882515464841,
20.0294039696079));
#203648=CARTESIAN_POINT('Ctrl Pts',(-20.0322750185584,20.8831959448388,
20.0289062961787));
#203649=CARTESIAN_POINT('Ctrl Pts',(-20.0459563402021,20.872488048422,20.027856890871));
#203650=CARTESIAN_POINT('Ctrl Pts',(-20.0530931163535,20.866827684261,20.0273048427003));
#203651=CARTESIAN_POINT('Ctrl Pts',(-20.071994794807,20.8516365152644,20.0258302504324));
#203652=CARTESIAN_POINT('Ctrl Pts',(-20.0836941922862,20.8420253875333,
20.0249044937169));
#203653=CARTESIAN_POINT('Ctrl Pts',(-20.1190566220114,20.8123339060278,
20.0220657955205));
#203654=CARTESIAN_POINT('Ctrl Pts',(-20.1423812652576,20.7918586841645,
20.0201370322303));
#203655=CARTESIAN_POINT('Ctrl Pts',(-20.2893760931676,20.6569855062784,
20.0076101401539));
#203656=CARTESIAN_POINT('Ctrl Pts',(-20.3994520606363,20.5286955146946,
19.9964221181894));
#203657=CARTESIAN_POINT('Ctrl Pts',(-20.5482381121422,20.3064614442645,
19.9788043017855));
#203658=CARTESIAN_POINT('Ctrl Pts',(-20.597495842582,20.220397644303,19.9723516834433));
#203659=CARTESIAN_POINT('Ctrl Pts',(-20.6447646744775,20.1224611048589,
19.9656327945442));
#203660=CARTESIAN_POINT('Ctrl Pts',(-20.648918711576,20.1137011261553,19.9650371214703));
#203661=CARTESIAN_POINT('Ctrl Pts',(-20.6549630916588,20.1007253169797,
19.9641629148744));
#203662=CARTESIAN_POINT('Ctrl Pts',(-20.6568999796039,20.0965314836658,
19.9638816154837));
#203663=CARTESIAN_POINT('Ctrl Pts',(-20.6603117270737,20.0890802442637,
19.9633840817029));
#203664=CARTESIAN_POINT('Ctrl Pts',(-20.6617920753913,20.085825411134,19.9631675124284));
#203665=CARTESIAN_POINT('Ctrl Pts',(-20.6649460109109,20.0788439897306,
19.9627046254899));
#203666=CARTESIAN_POINT('Ctrl Pts',(-20.6666170558024,20.0751163138345,
19.9624584640114));
#203667=CARTESIAN_POINT('Ctrl Pts',(-20.6711741838904,20.0648711771758,
19.9617845754104));
#203668=CARTESIAN_POINT('Ctrl Pts',(-20.6740381883078,20.0583438718376,
19.9613581802235));
#203669=CARTESIAN_POINT('Ctrl Pts',(-20.6891489403583,20.0234269582299,
19.9590922948952));
#203670=CARTESIAN_POINT('Ctrl Pts',(-20.7008063068103,19.9947844856062,
19.9572865274356));
#203671=CARTESIAN_POINT('Ctrl Pts',(-20.7154851133572,19.956325874309,19.9549187250179));
#203672=CARTESIAN_POINT('Ctrl Pts',(-20.7190678396831,19.9467306315134,
19.9543326139909));
#203673=CARTESIAN_POINT('Ctrl Pts',(-20.7225806070201,19.9371103011137,
19.9537492499338));
#203674=CARTESIAN_POINT('',(-20.8509996091577,19.2097135994841,20.489056279057));
#203675=CARTESIAN_POINT('Ctrl Pts',(-20.7225805741668,19.9371103910883,
19.7345261348292));
#203676=CARTESIAN_POINT('Ctrl Pts',(-20.6874528645367,20.0333137808797,
19.7401269736001));
#203677=CARTESIAN_POINT('Ctrl Pts',(-20.6453763458548,20.1268797428984,
19.7456315769633));
#203678=CARTESIAN_POINT('Ctrl Pts',(-20.5472451465103,20.3085633188397,
19.7569907920168));
#203679=CARTESIAN_POINT('Ctrl Pts',(-20.4911568811255,20.3962842901653,
19.7628329049756));
#203680=CARTESIAN_POINT('Ctrl Pts',(-20.4204318604439,20.4907789784509,
19.7697496500948));
#203681=CARTESIAN_POINT('Ctrl Pts',(-20.4118958786208,20.5019500609643,
19.7705777418217));
#203682=CARTESIAN_POINT('Ctrl Pts',(-20.398090742683,20.5196486737819,19.771906854087));
#203683=CARTESIAN_POINT('Ctrl Pts',(-20.3928928706097,20.5262314594874,
19.7724050529998));
#203684=CARTESIAN_POINT('Ctrl Pts',(-20.3836314069099,20.5378182891011,
19.7732888969456));
#203685=CARTESIAN_POINT('Ctrl Pts',(-20.3795837994358,20.5428350155228,
19.7736738979507));
#203686=CARTESIAN_POINT('Ctrl Pts',(-20.3711396544079,20.55320368208,19.7744745067719));
#203687=CARTESIAN_POINT('Ctrl Pts',(-20.3667396426101,20.5585526816788,
19.7748902526454));
#203688=CARTESIAN_POINT('Ctrl Pts',(-20.3553245519944,20.5722917767487,
19.7759652279275));
#203689=CARTESIAN_POINT('Ctrl Pts',(-20.3482706301432,20.5806491996022,
19.776626039594));
#203690=CARTESIAN_POINT('Ctrl Pts',(-20.3180882549007,20.6158519458345,
19.7794392765532));
#203691=CARTESIAN_POINT('Ctrl Pts',(-20.2943535689076,20.6421677367845,
19.7816167106324));
#203692=CARTESIAN_POINT('Ctrl Pts',(-20.2303134738308,20.7096846878417,
19.7874064274032));
#203693=CARTESIAN_POINT('Ctrl Pts',(-20.1889686577498,20.7498551199264,
19.7910612723479));
#203694=CARTESIAN_POINT('Ctrl Pts',(-20.0462318602119,20.8776378722556,
19.8034000038617));
#203695=CARTESIAN_POINT('Ctrl Pts',(-19.9381729570585,20.9573094284539,
19.8123264104771));
#203696=CARTESIAN_POINT('Ctrl Pts',(-19.7463729164797,21.0724091967956,
19.8270272051316));
#203697=CARTESIAN_POINT('Ctrl Pts',(-19.6665527321374,21.1136540115788,
19.8328477324719));
#203698=CARTESIAN_POINT('Ctrl Pts',(-19.57550799869,21.1535875640848,19.8389897336681));
#203699=CARTESIAN_POINT('Ctrl Pts',(-19.5666425092047,21.1574040217694,
19.8395827352411));
#203700=CARTESIAN_POINT('Ctrl Pts',(-19.5535033405703,21.1629540304545,
19.8404537836909));
#203701=CARTESIAN_POINT('Ctrl Pts',(-19.5492497457969,21.1647344023998,
19.8407345682682));
#203702=CARTESIAN_POINT('Ctrl Pts',(-19.5416882441973,21.167870327662,19.8412315338358));
#203703=CARTESIAN_POINT('Ctrl Pts',(-19.5383826911072,21.1692314127856,
19.8414480468562));
#203704=CARTESIAN_POINT('Ctrl Pts',(-19.531287447963,21.1721319323638,19.8419111928304));
#203705=CARTESIAN_POINT('Ctrl Pts',(-19.5274967500655,21.1736687542994,
19.8421576676146));
#203706=CARTESIAN_POINT('Ctrl Pts',(-19.5170660107303,21.1778624179042,
19.8428332971481));
#203707=CARTESIAN_POINT('Ctrl Pts',(-19.5104168523787,21.180496641985,19.8432611084763));
#203708=CARTESIAN_POINT('Ctrl Pts',(-19.4746420261715,21.1944603701148,
19.845548135564));
#203709=CARTESIAN_POINT('Ctrl Pts',(-19.4452798777489,21.2051782317934,
19.847372878789));
#203710=CARTESIAN_POINT('Ctrl Pts',(-19.260629078845,21.2679822568139,19.8585873624618));
#203711=CARTESIAN_POINT('Ctrl Pts',(-19.0999557890122,21.3025551348048,
19.8672422485546));
#203712=CARTESIAN_POINT('Ctrl Pts',(-18.8202504278169,21.3294853923018,
19.8826237568739));
#203713=CARTESIAN_POINT('Ctrl Pts',(-18.7028972239463,21.3310110417204,
19.8891641172679));
#203714=CARTESIAN_POINT('Ctrl Pts',(-18.5717696863479,21.321823217635,19.8968647966411));
#203715=CARTESIAN_POINT('Ctrl Pts',(-18.5575209697598,21.3206797073814,
19.8977065677578));
#203716=CARTESIAN_POINT('Ctrl Pts',(-18.5348635439064,21.3186302275625,
19.8990534900374));
#203717=CARTESIAN_POINT('Ctrl Pts',(-18.526446641612,21.3178180046074,19.8995556976312));
#203718=CARTESIAN_POINT('Ctrl Pts',(-18.5116115659835,21.3162966721673,
19.9004441996928));
#203719=CARTESIAN_POINT('Ctrl Pts',(-18.505191311686,21.3156085802708,19.9008298277014));
#203720=CARTESIAN_POINT('Ctrl Pts',(-18.49191942482,21.3141247163812,19.901629324225));
#203721=CARTESIAN_POINT('Ctrl Pts',(-18.4850683402041,21.3133248094747,
19.9020433188774));
#203722=CARTESIAN_POINT('Ctrl Pts',(-18.467493998862,21.3111857851513,19.9031086533977));
#203723=CARTESIAN_POINT('Ctrl Pts',(-18.4567769623727,21.3097980277819,
19.9037615217948));
#203724=CARTESIAN_POINT('Ctrl Pts',(-18.4121028993987,21.3036650105896,
19.9064967342604));
#203725=CARTESIAN_POINT('Ctrl Pts',(-18.3782546071803,21.2981774216519,
19.9086023915845));
#203726=CARTESIAN_POINT('Ctrl Pts',(-18.2904310922278,21.2817408669927,
19.9141559958322));
#203727=CARTESIAN_POINT('Ctrl Pts',(-18.2367260743028,21.2695040533783,
19.917642313157));
#203728=CARTESIAN_POINT('Ctrl Pts',(-18.0779619707337,21.2267537357433,
19.9282103742442));
#203729=CARTESIAN_POINT('Ctrl Pts',(-17.9747307738845,21.1901805866374,
19.9354405137537));
#203730=CARTESIAN_POINT('Ctrl Pts',(-17.8336070264534,21.1275105133743,
19.9456407028877));
#203731=CARTESIAN_POINT('Ctrl Pts',(-17.7930121217363,21.1079085505382,
19.9486123189255));
#203732=CARTESIAN_POINT('Ctrl Pts',(-17.7315240442198,21.0757579661745,
19.9531457788603));
#203733=CARTESIAN_POINT('Ctrl Pts',(-17.7101701880462,21.0641197732191,
19.9547263472012));
#203734=CARTESIAN_POINT('Ctrl Pts',(-17.6764762065792,21.0449957732786,
19.9572253256428));
#203735=CARTESIAN_POINT('Ctrl Pts',(-17.664004201647,21.0377474042532,19.9581514497857));
#203736=CARTESIAN_POINT('Ctrl Pts',(-17.6196457580066,21.0113573810365,
19.961446908818));
#203737=CARTESIAN_POINT('Ctrl Pts',(-17.5881887951268,20.9915024986112,
19.9637868957674));
#203738=CARTESIAN_POINT('Ctrl Pts',(-17.5513117985625,20.9668442349921,
19.9665188397064));
#203739=CARTESIAN_POINT('Ctrl Pts',(-17.5453745339745,20.9628304325025,
19.9669583295065));
#203740=CARTESIAN_POINT('Ctrl Pts',(-17.5357261091608,20.9562361191214,
19.9676717902986));
#203741=CARTESIAN_POINT('Ctrl Pts',(-17.5320026849954,20.9536737745633,
19.9679469414648));
#203742=CARTESIAN_POINT('Ctrl Pts',(-17.5253558873047,20.9490682176025,
19.968437756491));
#203743=CARTESIAN_POINT('Ctrl Pts',(-17.5224294544831,20.9470295314428,
19.9686537211069));
#203744=CARTESIAN_POINT('Ctrl Pts',(-17.5161070028874,20.9426012502507,
19.9691200171473));
#203745=CARTESIAN_POINT('Ctrl Pts',(-17.5127128690109,20.940209063892,19.9693701674822));
#203746=CARTESIAN_POINT('Ctrl Pts',(-17.5032615164751,20.9335060399016,
19.9700663160942));
#203747=CARTESIAN_POINT('Ctrl Pts',(-17.497219866501,20.9291732093798,19.970510832222));
#203748=CARTESIAN_POINT('Ctrl Pts',(-17.4624537730576,20.9039619549484,
19.9730667204714));
#203749=CARTESIAN_POINT('Ctrl Pts',(-17.4342336170357,20.8823939310384,
19.9751333153187));
#203750=CARTESIAN_POINT('Ctrl Pts',(-17.3456225008949,20.8110680574318,
19.9816435231452));
#203751=CARTESIAN_POINT('Ctrl Pts',(-17.2874386481221,20.7586666397095,
19.9859522075909));
#203752=CARTESIAN_POINT('Ctrl Pts',(-17.0994165507255,20.569440708076,20.0005035983331));
#203753=CARTESIAN_POINT('Ctrl Pts',(-16.9850164731049,20.4185906179988,
20.0105710568498));
#203754=CARTESIAN_POINT('Ctrl Pts',(-16.8813488187142,20.2356209234951,
20.0228057707912));
#203755=CARTESIAN_POINT('Ctrl Pts',(-16.8708941611175,20.2164854635343,
20.0240842277369));
#203756=CARTESIAN_POINT('Ctrl Pts',(-16.8568190163854,20.1897498653763,
20.0258704203196));
#203757=CARTESIAN_POINT('Ctrl Pts',(-16.8529452524452,20.1822840870812,
20.0263691989217));
#203758=CARTESIAN_POINT('Ctrl Pts',(-16.8463547618638,20.1693951397965,
20.0272303673294));
#203759=CARTESIAN_POINT('Ctrl Pts',(-16.8436166441755,20.1639829777535,
20.027592000695));
#203760=CARTESIAN_POINT('Ctrl Pts',(-16.8380122020275,20.1527860420176,
20.0283402463647));
#203761=CARTESIAN_POINT('Ctrl Pts',(-16.8351490080665,20.1469997799148,
20.0287269633922));
#203762=CARTESIAN_POINT('Ctrl Pts',(-16.8285349301214,20.1334780611912,
20.0296308165883));
#203763=CARTESIAN_POINT('Ctrl Pts',(-16.8248046292708,20.1257327144509,
20.0301486628408));
#203764=CARTESIAN_POINT('Ctrl Pts',(-16.812964708747,20.1007611566909,20.031818719909));
#203765=CARTESIAN_POINT('Ctrl Pts',(-16.805040443855,20.0834485656936,20.0329773029342));
#203766=CARTESIAN_POINT('Ctrl Pts',(-16.7663465140776,19.9958067320823,
20.0388477162392));
#203767=CARTESIAN_POINT('Ctrl Pts',(-16.7391880485159,19.9239550022546,
20.0436805596129));
#203768=CARTESIAN_POINT('Ctrl Pts',(-16.6822908531277,19.7444926184962,
20.0557898003521));
#203769=CARTESIAN_POINT('Ctrl Pts',(-16.6570431131656,19.6357014647624,
20.0631697140928));
#203770=CARTESIAN_POINT('Ctrl Pts',(-16.6293970110739,19.4516347686704,
20.0754613631624));
#203771=CARTESIAN_POINT('Ctrl Pts',(-16.6222218536133,19.3772923795296,
20.0803704675103));
#203772=CARTESIAN_POINT('Ctrl Pts',(-16.6171535358165,19.2604232395742,
20.0878711166196));
#203773=CARTESIAN_POINT('Ctrl Pts',(-16.6165883462097,19.2180748651562,
20.0905441807989));
#203774=CARTESIAN_POINT('Ctrl Pts',(-16.6174179332694,19.1682807342008,
20.0936130481782));
#203775=CARTESIAN_POINT('Ctrl Pts',(-16.6175815007662,19.1608270915809,
20.0940704648653));
#203776=CARTESIAN_POINT('Ctrl Pts',(-16.6179098542651,19.1487688032113,
20.0948071204086));
#203777=CARTESIAN_POINT('Ctrl Pts',(-16.6180503012006,19.1441636340961,
20.0950876673628));
#203778=CARTESIAN_POINT('Ctrl Pts',(-16.6183264053844,19.1359865522908,
20.0955843708287));
#203779=CARTESIAN_POINT('Ctrl Pts',(-16.6184560758463,19.1324144928156,
20.0958008580551));
#203780=CARTESIAN_POINT('Ctrl Pts',(-16.6187536301728,19.1247529952551,
20.0962641244538));
#203781=CARTESIAN_POINT('Ctrl Pts',(-16.6189243255965,19.1206637221614,
20.0965107445366));
#203782=CARTESIAN_POINT('Ctrl Pts',(-16.6194263708169,19.1094191238481,
20.0971871832219));
#203783=CARTESIAN_POINT('Ctrl Pts',(-16.619782181935,19.102264868829,20.0976156530432));
#203784=CARTESIAN_POINT('Ctrl Pts',(-16.6218936123549,19.0637517105565,
20.0999126006471));
#203785=CARTESIAN_POINT('Ctrl Pts',(-16.6243107150034,19.0324312192418,
20.1017462509021));
#203786=CARTESIAN_POINT('Ctrl Pts',(-16.6436439148964,18.8383327301782,
20.1129599034163));
#203787=CARTESIAN_POINT('Ctrl Pts',(-16.6786921959594,18.6779038018545,
20.1216078327003));
#203788=CARTESIAN_POINT('Ctrl Pts',(-16.7699426851546,18.4123204300067,
20.1369798811944));
#203789=CARTESIAN_POINT('Ctrl Pts',(-16.8171287102505,18.3049043318235,
20.1435181531083));
#203790=CARTESIAN_POINT('Ctrl Pts',(-16.8797636682858,18.1893831726543,
20.1512164811181));
#203791=CARTESIAN_POINT('Ctrl Pts',(-16.8867037059908,18.1768869969954,
20.1520582216722));
#203792=CARTESIAN_POINT('Ctrl Pts',(-16.8979497820688,18.1571119135259,
20.1534051037197));
#203793=CARTESIAN_POINT('Ctrl Pts',(-16.9021738860903,18.1497867382985,
20.1539073019108));
#203794=CARTESIAN_POINT('Ctrl Pts',(-16.9097007604109,18.13691295632,20.1547957924554));
#203795=CARTESIAN_POINT('Ctrl Pts',(-16.9129852621242,18.1313537542417,
20.1551814183988));
#203796=CARTESIAN_POINT('Ctrl Pts',(-16.9198309274037,18.1198871945549,
20.1559809156624));
#203797=CARTESIAN_POINT('Ctrl Pts',(-16.9233956286274,18.1139820481023,
20.1563949131447));
#203798=CARTESIAN_POINT('Ctrl Pts',(-16.9326191540797,18.098870136136,20.157460265513));
#203799=CARTESIAN_POINT('Ctrl Pts',(-16.9383196809577,18.0896891728121,
20.1581131490353));
#203800=CARTESIAN_POINT('Ctrl Pts',(-16.9624000762208,18.0515611465621,
20.1608485144656));
#203801=CARTESIAN_POINT('Ctrl Pts',(-16.9814107292305,18.0230204644939,
20.1629543129613));
#203802=CARTESIAN_POINT('Ctrl Pts',(-17.0327382898508,17.9498773812034,
20.1685083796784));
#203803=CARTESIAN_POINT('Ctrl Pts',(-17.0661158288889,17.9060543159262,
20.1719950263878));
#203804=CARTESIAN_POINT('Ctrl Pts',(-17.1707700623992,17.7792311363261,
20.1825637171255));
#203805=CARTESIAN_POINT('Ctrl Pts',(-17.246805960605,17.7004039787809,20.1897941551204));
#203806=CARTESIAN_POINT('Ctrl Pts',(-17.4171986714331,17.5491443517543,
20.2048450423653));
#203807=CARTESIAN_POINT('Ctrl Pts',(-17.5122733757762,17.4780486079682,
20.2126374394778));
#203808=CARTESIAN_POINT('Ctrl Pts',(-17.6208857716582,17.4102344980526,
20.2205462053651));
#203809=CARTESIAN_POINT('Ctrl Pts',(-17.6289972541556,17.4052456928466,
20.2211311706908));
#203810=CARTESIAN_POINT('Ctrl Pts',(-17.6410646136959,17.3979356681566,
20.2219927084499));
#203811=CARTESIAN_POINT('Ctrl Pts',(-17.6449946851759,17.3955723767559,
20.2222719346882));
#203812=CARTESIAN_POINT('Ctrl Pts',(-17.6519998027772,17.3913908841978,
20.2227671848337));
#203813=CARTESIAN_POINT('Ctrl Pts',(-17.6550717964235,17.3895676808383,
20.2229835321382));
#203814=CARTESIAN_POINT('Ctrl Pts',(-17.6616852885319,17.3856652295397,
20.2234474857179));
#203815=CARTESIAN_POINT('Ctrl Pts',(-17.6652282160521,17.3835885139964,
20.2236949277196));
#203816=CARTESIAN_POINT('Ctrl Pts',(-17.6750217721551,17.3778861661999,
20.2243759439892));
#203817=CARTESIAN_POINT('Ctrl Pts',(-17.6812850229684,17.3742821677578,
20.2248081389945));
#203818=CARTESIAN_POINT('Ctrl Pts',(-17.7156527973087,17.3547398194418,
20.2271621837761));
#203819=CARTESIAN_POINT('Ctrl Pts',(-17.7441025606535,17.3394134538812,
20.229047125599));
#203820=CARTESIAN_POINT('Ctrl Pts',(-17.9180134275817,17.250800467562,20.2402567665192));
#203821=CARTESIAN_POINT('Ctrl Pts',(-18.0711964126083,17.1938436787367,
20.2488651981567));
#203822=CARTESIAN_POINT('Ctrl Pts',(-18.3429424056517,17.1271504400649,
20.2641830549628));
#203823=CARTESIAN_POINT('Ctrl Pts',(-18.4585725957482,17.1087418074613,
20.2707089322401));
#203824=CARTESIAN_POINT('Ctrl Pts',(-18.5893728266064,17.0988976800505,
20.2783933096479));
#203825=CARTESIAN_POINT('Ctrl Pts',(-18.6036336292863,17.0979695166197,
20.279234874441));
#203826=CARTESIAN_POINT('Ctrl Pts',(-18.6263447455836,17.0967221485764,
20.280581528103));
#203827=CARTESIAN_POINT('Ctrl Pts',(-18.6347896167472,17.0963090572107,
20.2810836752558));
#203828=CARTESIAN_POINT('Ctrl Pts',(-18.64968757838,17.0956697405005,20.2819721067216));
#203829=CARTESIAN_POINT('Ctrl Pts',(-18.6561396898981,17.0954224283003,
20.282357724913));
#203830=CARTESIAN_POINT('Ctrl Pts',(-18.6694869113169,17.0949719650697,
20.2831572367602));
#203831=CARTESIAN_POINT('Ctrl Pts',(-18.6763820769847,17.0947729903392,
20.2835712567292));
#203832=CARTESIAN_POINT('Ctrl Pts',(-18.6940833346544,17.0943487577032,
20.2846367315312));
#203833=CARTESIAN_POINT('Ctrl Pts',(-18.70489030412,17.0941725529676,20.2852897156728));
#203834=CARTESIAN_POINT('Ctrl Pts',(-18.7500000923134,17.0937825527587,
20.2880260518357));
#203835=CARTESIAN_POINT('Ctrl Pts',(-18.7843026335893,17.0943197807308,
20.290132741089));
#203836=CARTESIAN_POINT('Ctrl Pts',(-18.8736326308795,17.0978914215381,
20.2956897176309));
#203837=CARTESIAN_POINT('Ctrl Pts',(-18.9285787366785,17.1022412583556,
20.2991784334485));
#203838=CARTESIAN_POINT('Ctrl Pts',(-19.0871592007349,17.1210458663305,
20.309442931949));
#203839=CARTESIAN_POINT('Ctrl Pts',(-19.1899664820562,17.1410431983778,
20.3163493047314));
#203840=CARTESIAN_POINT('Ctrl Pts',(-19.4098671599444,17.2009983945365,
20.3314098294747));
#203841=CARTESIAN_POINT('Ctrl Pts',(-19.5258188950069,17.243785553549,20.339539024291));
#203842=CARTESIAN_POINT('Ctrl Pts',(-19.6459307954948,17.3004607260458,
20.3477410089447));
#203843=CARTESIAN_POINT('Ctrl Pts',(-19.6544402859681,17.3045457570014,
20.3483207756051));
#203844=CARTESIAN_POINT('Ctrl Pts',(-19.6670283912397,17.3106926825183,
20.3491761548535));
#203845=CARTESIAN_POINT('Ctrl Pts',(-19.6711279760125,17.3127110237867,
20.3494543675911));
#203846=CARTESIAN_POINT('Ctrl Pts',(-19.6784194657484,17.3163302073944,
20.3499485095131));
#203847=CARTESIAN_POINT('Ctrl Pts',(-19.6816138794697,17.3179258634747,
20.3501647564579));
#203848=CARTESIAN_POINT('Ctrl Pts',(-19.688409416523,17.3213418440018,20.3506242685243));
#203849=CARTESIAN_POINT('Ctrl Pts',(-19.6920093650211,17.3231643773795,
20.3508673923215));
#203850=CARTESIAN_POINT('Ctrl Pts',(-19.7018355054494,17.328174368415,20.3515302328636));
#203851=CARTESIAN_POINT('Ctrl Pts',(-19.7080512103204,17.331382441201,20.3519486756186));
#203852=CARTESIAN_POINT('Ctrl Pts',(-19.7219082459135,17.3386215838536,
20.3528798861944));
#203853=CARTESIAN_POINT('Ctrl Pts',(-19.72954107462,17.3426687633563,20.3533916941851));
#203854=CARTESIAN_POINT('Ctrl Pts',(-19.7529959856932,17.3552898877915,
20.3549616005021));
#203855=CARTESIAN_POINT('Ctrl Pts',(-19.7687340848304,17.3640191508954,
20.3560110062428));
#203856=CARTESIAN_POINT('Ctrl Pts',(-19.8288875693707,17.3983940185225,
20.3600139473651));
#203857=CARTESIAN_POINT('Ctrl Pts',(-19.8724793884733,17.4254511703355,
20.3628978631502));
#203858=CARTESIAN_POINT('Ctrl Pts',(-20.0283843359217,17.5302538040623,
20.373307393401));
#203859=CARTESIAN_POINT('Ctrl Pts',(-20.1340846186065,17.6172296022106,
20.3805736985629));
#203860=CARTESIAN_POINT('Ctrl Pts',(-20.3002739040948,17.7833585882957,
20.3935317161442));
#203861=CARTESIAN_POINT('Ctrl Pts',(-20.3649301418683,17.8576939485678,
20.3990753213143));
#203862=CARTESIAN_POINT('Ctrl Pts',(-20.4325720095384,17.9473796252565,
20.405659270609));
#203863=CARTESIAN_POINT('Ctrl Pts',(-20.4408556706767,17.958591508861,20.4064804514039));
#203864=CARTESIAN_POINT('Ctrl Pts',(-20.4539248241869,17.9766510340835,
20.4078005605493));
#203865=CARTESIAN_POINT('Ctrl Pts',(-20.4587816472569,17.9834467275316,
20.4082967280098));
#203866=CARTESIAN_POINT('Ctrl Pts',(-20.4673119315461,17.9955329171899,
20.4091782237183));
#203867=CARTESIAN_POINT('Ctrl Pts',(-20.4710017251783,18.0008117969722,
20.4095629192933));
#203868=CARTESIAN_POINT('Ctrl Pts',(-20.4786180326546,18.0118148171145,
20.4103641471899));
#203869=CARTESIAN_POINT('Ctrl Pts',(-20.4825405921835,18.017541589155,20.410780823781));
#203870=CARTESIAN_POINT('Ctrl Pts',(-20.4926091153895,18.0323973991309,
20.411860903163));
#203871=CARTESIAN_POINT('Ctrl Pts',(-20.4987121274749,18.0415551695413,
20.4125259168787));
#203872=CARTESIAN_POINT('Ctrl Pts',(-20.5245037155325,18.0809179587915,
20.415381281402));
#203873=CARTESIAN_POINT('Ctrl Pts',(-20.5434893668762,18.1115742610356,
20.4175975827553));
#203874=CARTESIAN_POINT('Ctrl Pts',(-20.5914726758973,18.1936655763423,
20.4235165806251));
#203875=CARTESIAN_POINT('Ctrl Pts',(-20.6191159820387,18.2458519230385,
20.4272642400987));
#203876=CARTESIAN_POINT('Ctrl Pts',(-20.7103286358132,18.4369579849455,
20.4409173756229));
#203877=CARTESIAN_POINT('Ctrl Pts',(-20.761004583689,18.5815065457925,20.4511535737685));
#203878=CARTESIAN_POINT('Ctrl Pts',(-20.8019773254567,18.7572088796499,
20.4629187575841));
#203879=CARTESIAN_POINT('Ctrl Pts',(-20.8077392299131,18.7843123994527,
20.464713888162));
#203880=CARTESIAN_POINT('Ctrl Pts',(-20.8211288701866,18.8539949184674,
20.4692668936239));
#203881=CARTESIAN_POINT('Ctrl Pts',(-20.8279872952478,18.8967113660204,
20.4719990528603));
#203882=CARTESIAN_POINT('Ctrl Pts',(-20.834494318318,18.9470513297185,20.4751272534771));
#203883=CARTESIAN_POINT('Ctrl Pts',(-20.8354165132923,18.9544967381812,
20.4755875809307));
#203884=CARTESIAN_POINT('Ctrl Pts',(-20.8368427998261,18.9665362684793,
20.4763279959977));
#203885=CARTESIAN_POINT('Ctrl Pts',(-20.8373714516943,18.9711273380694,
20.4766094130056));
#203886=CARTESIAN_POINT('Ctrl Pts',(-20.8382824844706,18.9792738422144,
20.4771070767456));
#203887=CARTESIAN_POINT('Ctrl Pts',(-20.8386708949005,18.9828285480352,
20.47732365902));
#203888=CARTESIAN_POINT('Ctrl Pts',(-20.8394063458069,18.9897210366878,
20.4777424893418));
#203889=CARTESIAN_POINT('Ctrl Pts',(-20.8397544550189,18.993058640691,20.4779447988319));
#203890=CARTESIAN_POINT('Ctrl Pts',(-20.8405037123441,19.0004117879156,
20.4783894290261));
#203891=CARTESIAN_POINT('Ctrl Pts',(-20.8409013186364,19.0044276898395,
20.478631552258));
#203892=CARTESIAN_POINT('Ctrl Pts',(-20.8418560175519,19.0143599179749,
20.4792286755137));
#203893=CARTESIAN_POINT('Ctrl Pts',(-20.8423996911825,19.0202775401958,
20.4795829495));
#203894=CARTESIAN_POINT('Ctrl Pts',(-20.8445839025751,19.0452031904335,
20.4810692025915));
#203895=CARTESIAN_POINT('Ctrl Pts',(-20.8459924232064,19.064231299655,20.4821891524991));
#203896=CARTESIAN_POINT('Ctrl Pts',(-20.849686309312,19.125345466913,20.485746622392));
#203897=CARTESIAN_POINT('Ctrl Pts',(-20.8509723412172,19.1674831001617,
20.48813942538));
#203898=CARTESIAN_POINT('Ctrl Pts',(-20.8509995586411,19.2096329911406,
20.4904972704014));
#203899=CARTESIAN_POINT('Ctrl Pts',(-20.7225806064498,19.9371103026755,
20.5336910513061));
#203900=CARTESIAN_POINT('Ctrl Pts',(-20.7472974864126,19.8694187853333,
20.5293719591642));
#203901=CARTESIAN_POINT('Ctrl Pts',(-20.7685453196057,19.800487370849,20.5250528670223));
#203902=CARTESIAN_POINT('Ctrl Pts',(-20.7862158025195,19.7307107848498,
20.5207337748803));
#203903=CARTESIAN_POINT('Ctrl Pts',(-20.8038940120027,19.660903688443,20.5164127941785));
#203904=CARTESIAN_POINT('Ctrl Pts',(-20.8179916608039,19.5902511717225,
20.5120918134767));
#203905=CARTESIAN_POINT('Ctrl Pts',(-20.8284516779761,19.5191577008985,
20.5077708327749));
#203906=CARTESIAN_POINT('Ctrl Pts',(-20.8389271851641,19.4479589492739,
20.5034434532251));
#203907=CARTESIAN_POINT('Ctrl Pts',(-20.8457542653409,19.3763184341297,
20.4991160736754));
#203908=CARTESIAN_POINT('Ctrl Pts',(-20.8489278371988,19.3046442387004,
20.4947886941257));
#203909=CARTESIAN_POINT('Ctrl Pts',(-20.8503291649484,19.2729956599096,
20.4928778891028));
#203910=CARTESIAN_POINT('Ctrl Pts',(-20.8510188273247,19.2413404929336,
20.4909670840799));
#203911=CARTESIAN_POINT('Ctrl Pts',(-20.8509996091577,19.2097135994841,
20.489056279057));
#203912=CARTESIAN_POINT('Origin',(-18.734,19.211,0.));
#203913=CARTESIAN_POINT('',(-20.7225806064499,19.9371103026755,21.5555703710623));
#203914=CARTESIAN_POINT('',(-20.7225806064498,19.9371103026755,21.3335535417785));
#203915=CARTESIAN_POINT('',(-20.7225806064498,19.9371103026755,0.));
#203916=CARTESIAN_POINT('',(-20.8509993841528,19.2093852254739,21.5109437210328));
#203917=CARTESIAN_POINT('Ctrl Pts',(-20.8509993841528,19.2093852254739,
21.5109437210328));
#203918=CARTESIAN_POINT('Ctrl Pts',(-20.8510540319531,19.2810295063139,
21.515267181414));
#203919=CARTESIAN_POINT('Ctrl Pts',(-20.8474675450903,19.3528083048161,
21.5195906417951));
#203920=CARTESIAN_POINT('Ctrl Pts',(-20.8402254623162,19.4243150296886,
21.5239141021763));
#203921=CARTESIAN_POINT('Ctrl Pts',(-20.8329909780013,19.4957467290533,
21.5282330263434));
#203922=CARTESIAN_POINT('Ctrl Pts',(-20.8221085494476,19.5669064297487,
21.5325519505105));
#203923=CARTESIAN_POINT('Ctrl Pts',(-20.8076157375584,19.6373880544179,
21.5368708746776));
#203924=CARTESIAN_POINT('Ctrl Pts',(-20.7931333528068,19.7078189697004,
21.54118669151));
#203925=CARTESIAN_POINT('Ctrl Pts',(-20.7750458366717,19.7775722915727,
21.5455025083425));
#203926=CARTESIAN_POINT('Ctrl Pts',(-20.7534422764442,19.8462494723413,
21.5498183251749));
#203927=CARTESIAN_POINT('Ctrl Pts',(-20.74384465954,19.8767600578253,21.551735673804));
#203928=CARTESIAN_POINT('Ctrl Pts',(-20.7335537650588,19.9070583803701,
21.5536530224332));
#203929=CARTESIAN_POINT('Ctrl Pts',(-20.7225806064499,19.9371103026755,
21.5555703710623));
#203930=CARTESIAN_POINT('Ctrl Pts',(-20.8509994310935,19.209447985236,21.5099894778226));
#203931=CARTESIAN_POINT('Ctrl Pts',(-20.8509485247462,19.1400100451657,
21.5054226012226));
#203932=CARTESIAN_POINT('Ctrl Pts',(-20.8474812625977,19.070609682484,21.5009009210634));
#203933=CARTESIAN_POINT('Ctrl Pts',(-20.8382974076878,18.9782625879113,
21.4950376552809));
#203934=CARTESIAN_POINT('Ctrl Pts',(-20.8356021208678,18.955064636439,21.4935779570289));
#203935=CARTESIAN_POINT('Ctrl Pts',(-20.8317146611693,18.9258336681481,
21.4917592268508));
#203936=CARTESIAN_POINT('Ctrl Pts',(-20.8308794579723,18.9197558115299,
21.4913821951208));
#203937=CARTESIAN_POINT('Ctrl Pts',(-20.8294395976148,18.9096051687547,
21.4907544964862));
#203938=CARTESIAN_POINT('Ctrl Pts',(-20.8288494645369,18.9055304055484,
21.490503054755));
#203939=CARTESIAN_POINT('Ctrl Pts',(-20.8277537217301,18.8981170278529,
21.4900466025938));
#203940=CARTESIAN_POINT('Ctrl Pts',(-20.8272520064267,18.8947778637144,
21.4898413773219));
#203941=CARTESIAN_POINT('Ctrl Pts',(-20.8262053651731,18.8879235964327,
21.4894208972805));
#203942=CARTESIAN_POINT('Ctrl Pts',(-20.8256595713239,18.8844086792437,
21.4892056988165));
#203943=CARTESIAN_POINT('Ctrl Pts',(-20.8244066210198,18.8764716559245,
21.4887207236645));
#203944=CARTESIAN_POINT('Ctrl Pts',(-20.8236942930991,18.872050421987,21.4884512443155));
#203945=CARTESIAN_POINT('Ctrl Pts',(-20.8214988526174,18.8586939146337,
21.487639087692));
#203946=CARTESIAN_POINT('Ctrl Pts',(-20.8199723987706,18.8497657329395,
21.4870988243196));
#203947=CARTESIAN_POINT('Ctrl Pts',(-20.8078162681548,18.7813126038274,
21.4829748366242));
#203948=CARTESIAN_POINT('Ctrl Pts',(-20.7946969717277,18.7222520052379,
21.4795225738979));
#203949=CARTESIAN_POINT('Ctrl Pts',(-20.7741789047046,18.6455652344342,
21.4750848284973));
#203950=CARTESIAN_POINT('Ctrl Pts',(-20.769047825688,18.6273675720153,21.4740351573819));
#203951=CARTESIAN_POINT('Ctrl Pts',(-20.7520373438111,18.5699929222378,
21.4707297776502));
#203952=CARTESIAN_POINT('Ctrl Pts',(-20.7392648735595,18.5310899039518,
21.4684945105134));
#203953=CARTESIAN_POINT('Ctrl Pts',(-20.7134212063805,18.4594543385383,
21.4643518162005));
#203954=CARTESIAN_POINT('Ctrl Pts',(-20.7006455075783,18.426631045212,21.4624429242906));
#203955=CARTESIAN_POINT('Ctrl Pts',(-20.6589745566515,18.3269984218837,
21.456579322497));
#203956=CARTESIAN_POINT('Ctrl Pts',(-20.6274493266644,18.2613501573964,
21.4526165474976));
#203957=CARTESIAN_POINT('Ctrl Pts',(-20.5661683690656,18.1489747119488,
21.4455035834002));
#203958=CARTESIAN_POINT('Ctrl Pts',(-20.5378440241279,18.1015475542015,
21.4423912149869));
#203959=CARTESIAN_POINT('Ctrl Pts',(-20.4889707173757,18.0265407422782,
21.437242441228));
#203960=CARTESIAN_POINT('Ctrl Pts',(-20.46954686055,17.9982581275559,21.4352459080517));
#203961=CARTESIAN_POINT('Ctrl Pts',(-20.4431388058229,17.9617404747413,
21.4325885652031));
#203962=CARTESIAN_POINT('Ctrl Pts',(-20.4367661202885,17.9530682243842,
21.4319514493151));
#203963=CARTESIAN_POINT('Ctrl Pts',(-20.4262258339138,17.9389513638011,
21.4309042074722));
#203964=CARTESIAN_POINT('Ctrl Pts',(-20.4220973657203,17.9334776761409,
21.4304956227199));
#203965=CARTESIAN_POINT('Ctrl Pts',(-20.4140585606519,17.9229265147463,
21.4297030757405));
#203966=CARTESIAN_POINT('Ctrl Pts',(-20.410151609093,17.9178465471731,21.4293192505649));
#203967=CARTESIAN_POINT('Ctrl Pts',(-20.401083684171,17.9061662213702,21.4284314840878));
#203968=CARTESIAN_POINT('Ctrl Pts',(-20.3959064983369,17.8995786384633,
21.4279268969342));
#203969=CARTESIAN_POINT('Ctrl Pts',(-20.3818932538587,17.8819640741492,
21.4265670672812));
#203970=CARTESIAN_POINT('Ctrl Pts',(-20.3729857877455,17.8709946863608,
21.4257089485314));
#203971=CARTESIAN_POINT('Ctrl Pts',(-20.2682893331065,17.7446685562268,
21.4156928918964));
#203972=CARTESIAN_POINT('Ctrl Pts',(-20.1606339789355,17.6397358276293,
21.4060184879308));
#203973=CARTESIAN_POINT('Ctrl Pts',(-19.9681106254966,17.4882998852229,
21.3898622740542));
#203974=CARTESIAN_POINT('Ctrl Pts',(-19.8895235800659,17.4346299533531,
21.3835371506906));
#203975=CARTESIAN_POINT('Ctrl Pts',(-19.7687994158836,17.3635949698684,
21.3744153798713));
#203976=CARTESIAN_POINT('Ctrl Pts',(-19.7292832156593,17.3420090901545,
21.3715175443189));
#203977=CARTESIAN_POINT('Ctrl Pts',(-19.6670844694445,17.3105655023594,
21.3671223254294));
#203978=CARTESIAN_POINT('Ctrl Pts',(-19.6448684014709,17.2998179609983,
21.3655841816557));
#203979=CARTESIAN_POINT('Ctrl Pts',(-19.6165123943238,17.2867069007583,
21.3636654869528));
#203980=CARTESIAN_POINT('Ctrl Pts',(-19.6105435276297,17.2839806683043,
21.3632640753004));
#203981=CARTESIAN_POINT('Ctrl Pts',(-19.6014998841082,17.2799007700546,
21.3626597155254));
#203982=CARTESIAN_POINT('Ctrl Pts',(-19.5984344687366,17.2785266277516,
21.3624555260014));
#203983=CARTESIAN_POINT('Ctrl Pts',(-19.5921228733737,17.2757153343784,
21.3620364884064));
#203984=CARTESIAN_POINT('Ctrl Pts',(-19.588876396879,17.2742790730183,21.3618217028377));
#203985=CARTESIAN_POINT('Ctrl Pts',(-19.581585452878,17.2710754188185,21.3613410032991));
#203986=CARTESIAN_POINT('Ctrl Pts',(-19.5775390665966,17.2693125059526,
21.3610753655008));
#203987=CARTESIAN_POINT('Ctrl Pts',(-19.5672278349354,17.2648584674879,
21.3604012884986));
#203988=CARTESIAN_POINT('Ctrl Pts',(-19.5609553935305,17.2621849062964,
21.3599938957968));
#203989=CARTESIAN_POINT('Ctrl Pts',(-19.5252603478117,17.2471736430602,
21.3576899717216));
#203990=CARTESIAN_POINT('Ctrl Pts',(-19.4955730149619,17.2354712891341,
21.3558294172624));
#203991=CARTESIAN_POINT('Ctrl Pts',(-19.2794566073922,17.1558775630741,
21.3426052583473));
#203992=CARTESIAN_POINT('Ctrl Pts',(-19.0845512124342,17.1138151352113,
21.3322947409037));
#203993=CARTESIAN_POINT('Ctrl Pts',(-18.8308756325093,17.0954793164923,
21.3181606736389));
#203994=CARTESIAN_POINT('Ctrl Pts',(-18.7749971763512,17.0936594007002,
21.3150108109257));
#203995=CARTESIAN_POINT('Ctrl Pts',(-18.6844317030418,17.0942962020247,
21.3098016555587));
#203996=CARTESIAN_POINT('Ctrl Pts',(-18.6497613107883,17.0953923745127,
21.3077829610819));
#203997=CARTESIAN_POINT('Ctrl Pts',(-18.6042833866856,17.0979498994386,
21.3050967049045));
#203998=CARTESIAN_POINT('Ctrl Pts',(-18.593436913348,17.0986436997351,21.3044531783053));
#203999=CARTESIAN_POINT('Ctrl Pts',(-18.5756915912462,17.0999160676557,
21.3033954832749));
#204000=CARTESIAN_POINT('Ctrl Pts',(-18.5687893026128,17.1004450148345,
21.3029828742043));
#204001=CARTESIAN_POINT('Ctrl Pts',(-18.5554410671539,17.1015338186446,
21.3021825566981));
#204002=CARTESIAN_POINT('Ctrl Pts',(-18.5489948411741,17.1020893919963,
21.3017949870326));
#204003=CARTESIAN_POINT('Ctrl Pts',(-18.5341273125988,17.1034394533369,
21.3008985760075));
#204004=CARTESIAN_POINT('Ctrl Pts',(-18.5257080644039,17.1042548765098,
21.3003890824661));
#204005=CARTESIAN_POINT('Ctrl Pts',(-18.5031016628748,17.1065811933053,
21.2990159238409));
#204006=CARTESIAN_POINT('Ctrl Pts',(-18.4889247100316,17.1081850669386,
21.2981493541523));
#204007=CARTESIAN_POINT('Ctrl Pts',(-18.3611864329124,17.1239457148605,
21.2902910156079));
#204008=CARTESIAN_POINT('Ctrl Pts',(-18.2489491712357,17.1471434355782,
21.2830112441605));
#204009=CARTESIAN_POINT('Ctrl Pts',(-17.9820760906419,17.2252792964654,
21.2648705845793));
#204010=CARTESIAN_POINT('Ctrl Pts',(-17.8308695830361,17.2893258808947,
21.2538531237831));
#204011=CARTESIAN_POINT('Ctrl Pts',(-17.6600546573147,17.3863344394032,
21.2413709737737));
#204012=CARTESIAN_POINT('Ctrl Pts',(-17.6319353162539,17.4031790152025,
21.2393169273819));
#204013=CARTESIAN_POINT('Ctrl Pts',(-17.5980619654777,17.4245547172719,
21.2368539684987));
#204014=CARTESIAN_POINT('Ctrl Pts',(-17.5919271522271,17.4284704545616,
21.2364083701365));
#204015=CARTESIAN_POINT('Ctrl Pts',(-17.5823438714907,17.4346570692357,
21.2357131842111));
#204016=CARTESIAN_POINT('Ctrl Pts',(-17.5788817137874,17.4369064873755,
21.2354622172765));
#204017=CARTESIAN_POINT('Ctrl Pts',(-17.5724291994517,17.4411256832554,
21.2349948599569));
#204018=CARTESIAN_POINT('Ctrl Pts',(-17.5694372856936,17.4430929021827,
21.2347783105817));
#204019=CARTESIAN_POINT('Ctrl Pts',(-17.5626240950573,17.4475974570067,
21.2342855277546));
#204020=CARTESIAN_POINT('Ctrl Pts',(-17.5588060739463,17.4501396204159,
21.2340096221169));
#204021=CARTESIAN_POINT('Ctrl Pts',(-17.547098897815,17.4579896792205,21.2331642649505));
#204022=CARTESIAN_POINT('Ctrl Pts',(-17.5392370913703,17.4633384163671,
21.2325974878786));
#204023=CARTESIAN_POINT('Ctrl Pts',(-17.4690435160698,17.5117892757753,
21.2275427144372));
#204024=CARTESIAN_POINT('Ctrl Pts',(-17.4090248231839,17.5581614228085,
21.2232601553324));
#204025=CARTESIAN_POINT('Ctrl Pts',(-17.2444327716054,17.7000708042158,
21.2112299033746));
#204026=CARTESIAN_POINT('Ctrl Pts',(-17.1467844093052,17.802999092525,21.2037070623203));
#204027=CARTESIAN_POINT('Ctrl Pts',(-17.0222853102931,17.9637855823246,
21.1924562586107));
#204028=CARTESIAN_POINT('Ctrl Pts',(-16.9865976089396,18.014298279497,21.1889869012016));
#204029=CARTESIAN_POINT('Ctrl Pts',(-16.9330234364155,18.0976442436342,
21.1833006497682));
#204030=CARTESIAN_POINT('Ctrl Pts',(-16.913706115801,18.1295160434126,21.1811349016532));
#204031=CARTESIAN_POINT('Ctrl Pts',(-16.8897206261323,18.1715546343917,
21.1782817610181));
#204032=CARTESIAN_POINT('Ctrl Pts',(-16.8842770147697,18.1812728770676,
21.1776224368546));
#204033=CARTESIAN_POINT('Ctrl Pts',(-16.8755507543703,18.197143981157,21.1765458845813));
#204034=CARTESIAN_POINT('Ctrl Pts',(-16.8722213227779,18.2032709784969,
21.1761303343307));
#204035=CARTESIAN_POINT('Ctrl Pts',(-16.8658780886553,18.2150828726806,
21.1753292636372));
#204036=CARTESIAN_POINT('Ctrl Pts',(-16.8628598094832,18.2207652873432,
21.1749439080694));
#204037=CARTESIAN_POINT('Ctrl Pts',(-16.8560100733578,18.233804199237,21.1740596714827));
#204038=CARTESIAN_POINT('Ctrl Pts',(-16.8521958700176,18.2411695968248,
21.1735601876388));
#204039=CARTESIAN_POINT('Ctrl Pts',(-16.8421815755563,18.2607891535973,
21.1722296015074));
#204040=CARTESIAN_POINT('Ctrl Pts',(-16.8360573534164,18.2730814001101,
21.171395856851));
#204041=CARTESIAN_POINT('Ctrl Pts',(-16.7905178052886,18.3667588896692,
21.1650403450218));
#204042=CARTESIAN_POINT('Ctrl Pts',(-16.756238845878,18.4505243796976,21.1593417238349));
#204043=CARTESIAN_POINT('Ctrl Pts',(-16.6828169397694,18.6688559318926,
21.1444680071484));
#204044=CARTESIAN_POINT('Ctrl Pts',(-16.6514754114365,18.8055884718426,
21.1351165692679));
#204045=CARTESIAN_POINT('Ctrl Pts',(-16.6269181785219,18.9990359132272,
21.1223457036317));
#204046=CARTESIAN_POINT('Ctrl Pts',(-16.6221164443191,19.0539291383938,
21.118776421195));
#204047=CARTESIAN_POINT('Ctrl Pts',(-16.618091467603,19.1373295991591,21.1134917535915));
#204048=CARTESIAN_POINT('Ctrl Pts',(-16.6172932400701,19.1657349844734,
21.1117161606127));
#204049=CARTESIAN_POINT('Ctrl Pts',(-16.6170118442327,19.2010865739133,
21.1095435945588));
#204050=CARTESIAN_POINT('Ctrl Pts',(-16.6169907239664,19.2080241064856,
21.1091190261783));
#204051=CARTESIAN_POINT('Ctrl Pts',(-16.6170112722203,19.219004310664,21.1084500090418));
#204052=CARTESIAN_POINT('Ctrl Pts',(-16.6170304170123,19.2230469030434,
21.1082043308985));
#204053=CARTESIAN_POINT('Ctrl Pts',(-16.6170883600609,19.2306706474873,
21.1077422458833));
#204054=CARTESIAN_POINT('Ctrl Pts',(-16.6171246650422,19.2342517121927,
21.1075257080974));
#204055=CARTESIAN_POINT('Ctrl Pts',(-16.6172284509331,19.2424393599015,
21.107031779873));
#204056=CARTESIAN_POINT('Ctrl Pts',(-16.6173018816797,19.2470458195799,
21.1067547253964));
#204057=CARTESIAN_POINT('Ctrl Pts',(-16.6175368076541,19.2592775902263,
21.1060211791791));
#204058=CARTESIAN_POINT('Ctrl Pts',(-16.6177244757066,19.2669024106611,
21.1055661136631));
#204059=CARTESIAN_POINT('Ctrl Pts',(-16.6193295724009,19.3203679187707,
21.1023895689404));
#204060=CARTESIAN_POINT('Ctrl Pts',(-16.6221952109507,19.3661565922118,
21.0997432654898));
#204061=CARTESIAN_POINT('Ctrl Pts',(-16.6301239875518,19.4493632914149,
21.095011849846));
#204062=CARTESIAN_POINT('Ctrl Pts',(-16.6347043021177,19.4868063418828,
21.0929114942282));
#204063=CARTESIAN_POINT('Ctrl Pts',(-16.6596407163324,19.6535530483251,
21.0836113186086));
#204064=CARTESIAN_POINT('Ctrl Pts',(-16.6909611652801,19.7809240601643,
21.0766339409727));
#204065=CARTESIAN_POINT('Ctrl Pts',(-16.7627858596949,19.9880502685771,
21.0645332885749));
#204066=CARTESIAN_POINT('Ctrl Pts',(-16.7969196931691,20.0696091230245,
21.0595612073858));
#204067=CARTESIAN_POINT('Ctrl Pts',(-16.8451366468308,20.1671932288146,
21.0532176403441));
#204068=CARTESIAN_POINT('Ctrl Pts',(-16.8544955238402,20.1854604343622,
21.0520126238853));
#204069=CARTESIAN_POINT('Ctrl Pts',(-16.8682706978211,20.2114107181779,
21.0502742766851));
#204070=CARTESIAN_POINT('Ctrl Pts',(-16.8724721084835,20.2192069924006,
21.049748550832));
#204071=CARTESIAN_POINT('Ctrl Pts',(-16.8798389788427,20.2326741573723,
21.0488342821788));
#204072=CARTESIAN_POINT('Ctrl Pts',(-16.8829818648119,20.2383573078415,
21.0484465497055));
#204073=CARTESIAN_POINT('Ctrl Pts',(-16.8890741224098,20.2492549761701,
21.0476993358038));
#204074=CARTESIAN_POINT('Ctrl Pts',(-16.8920195799181,20.2544716192744,
21.0473399979043));
#204075=CARTESIAN_POINT('Ctrl Pts',(-16.8997915044371,20.2681008756961,
21.0463968010359));
#204076=CARTESIAN_POINT('Ctrl Pts',(-16.9046536700514,20.2764928750558,
21.0458116546712));
#204077=CARTESIAN_POINT('Ctrl Pts',(-16.9217170000874,20.3054827383888,
21.0437748245424));
#204078=CARTESIAN_POINT('Ctrl Pts',(-16.9342094177044,20.3259062392807,
21.0423125676579));
#204079=CARTESIAN_POINT('Ctrl Pts',(-17.0303110731261,20.4771945641552,
21.0312703117044));
#204080=CARTESIAN_POINT('Ctrl Pts',(-17.1277324331254,20.5986932536174,
21.0211541474364));
#204081=CARTESIAN_POINT('Ctrl Pts',(-17.2901177526393,20.7609737751704,
21.0059872620563));
#204082=CARTESIAN_POINT('Ctrl Pts',(-17.3454296123493,20.8107148113477,
21.0010640328941));
#204083=CARTESIAN_POINT('Ctrl Pts',(-17.4390019262775,20.8863455978038,
20.9932277997709));
#204084=CARTESIAN_POINT('Ctrl Pts',(-17.4756938277581,20.9140763357967,
20.9902669931262));
#204085=CARTESIAN_POINT('Ctrl Pts',(-17.5269183518952,20.9502303746368,
20.9863123308879));
#204086=CARTESIAN_POINT('Ctrl Pts',(-17.5406889084463,20.9597072587755,
20.9852661645677));
#204087=CARTESIAN_POINT('Ctrl Pts',(-17.5644673557033,20.9756598597418,
20.9834904517178));
#204088=CARTESIAN_POINT('Ctrl Pts',(-17.5744201527961,20.9822158591289,
20.9827562590566));
#204089=CARTESIAN_POINT('Ctrl Pts',(-17.5886443071773,20.9914141506185,
20.9817203841181));
#204090=CARTESIAN_POINT('Ctrl Pts',(-17.592870309317,20.9941256941223,20.9814142901151));
#204091=CARTESIAN_POINT('Ctrl Pts',(-17.6001689555432,20.9987721742109,
20.9808885589087));
#204092=CARTESIAN_POINT('Ctrl Pts',(-17.6032369892324,21.00071427846,20.9806684486337));
#204093=CARTESIAN_POINT('Ctrl Pts',(-17.6091968772973,21.0044655197048,
20.9802425986785));
#204094=CARTESIAN_POINT('Ctrl Pts',(-17.6120881041877,21.0062755592464,
20.9800367960242));
#204095=CARTESIAN_POINT('Ctrl Pts',(-17.6198977606497,21.011138525541,20.9794829645837));
#204096=CARTESIAN_POINT('Ctrl Pts',(-17.6248244002329,21.0141783055303,
20.9791357969227));
#204097=CARTESIAN_POINT('Ctrl Pts',(-17.6431400771674,21.025375771212,20.9778530778109));
#204098=CARTESIAN_POINT('Ctrl Pts',(-17.6566075193382,21.0334050827068,
20.9769255641445));
#204099=CARTESIAN_POINT('Ctrl Pts',(-17.7862406194556,21.1087531812253,
20.9681341967482));
#204100=CARTESIAN_POINT('Ctrl Pts',(-17.9084898030845,21.1650362866008,
20.9608716366963));
#204101=CARTESIAN_POINT('Ctrl Pts',(-18.1869543705648,21.2624029526393,
20.9448518903304));
#204102=CARTESIAN_POINT('Ctrl Pts',(-18.3441712705311,21.2979926668626,
20.9361045578553));
#204103=CARTESIAN_POINT('Ctrl Pts',(-18.5224425239592,21.3174853802441,
20.9256316224447));
#204104=CARTESIAN_POINT('Ctrl Pts',(-18.5410182405574,21.3192683013261,
20.9245344989187));
#204105=CARTESIAN_POINT('Ctrl Pts',(-18.5681149671023,21.3215079731011,
20.922924673644));
#204106=CARTESIAN_POINT('Ctrl Pts',(-18.5766193347084,21.3221591772313,
20.9224180773337));
#204107=CARTESIAN_POINT('Ctrl Pts',(-18.5915588554365,21.323212368742,20.9215256888576));
#204108=CARTESIAN_POINT('Ctrl Pts',(-18.5979923812902,21.323636385317,20.9211405933602));
#204109=CARTESIAN_POINT('Ctrl Pts',(-18.6105049471416,21.3244036632546,
20.9203900295935));
#204110=CARTESIAN_POINT('Ctrl Pts',(-18.6165837343203,21.3247501014283,
20.920024665026));
#204111=CARTESIAN_POINT('Ctrl Pts',(-18.6311455225416,21.3255169883941,
20.9191476478695));
#204112=CARTESIAN_POINT('Ctrl Pts',(-18.6396296753501,21.3259126167004,
20.918635221551));
#204113=CARTESIAN_POINT('Ctrl Pts',(-18.6704140468053,21.3271625302186,
20.9167705223329));
#204114=CARTESIAN_POINT('Ctrl Pts',(-18.6927244282053,21.3277152135136,
20.9154088546442));
#204115=CARTESIAN_POINT('Ctrl Pts',(-18.8983629617634,21.3295571239853,
20.9027594275979));
#204116=CARTESIAN_POINT('Ctrl Pts',(-19.0810913454143,21.3073779395509,
20.8906948008643));
#204117=CARTESIAN_POINT('Ctrl Pts',(-19.3376246637083,21.2417570241417,
20.8732107339467));
#204118=CARTESIAN_POINT('Ctrl Pts',(-19.4153876737813,21.217003345286,20.8678506049209));
#204119=CARTESIAN_POINT('Ctrl Pts',(-19.5255260965356,21.1747975052296,
20.8603296642829));
#204120=CARTESIAN_POINT('Ctrl Pts',(-19.5591797901394,21.1608956088291,
20.8580420257412));
#204121=CARTESIAN_POINT('Ctrl Pts',(-19.5993086988834,21.1430936790258,
20.8553410773665));
#204122=CARTESIAN_POINT('Ctrl Pts',(-19.6061409439404,21.1400192603111,
20.8548821771412));
#204123=CARTESIAN_POINT('Ctrl Pts',(-19.6167472360498,21.1351787018984,
20.8541714431051));
#204124=CARTESIAN_POINT('Ctrl Pts',(-19.6205325546415,21.1334376166326,
20.853918116734));
#204125=CARTESIAN_POINT('Ctrl Pts',(-19.6275486861944,21.1301853653737,
20.8534492210959));
#204126=CARTESIAN_POINT('Ctrl Pts',(-19.6307807916059,21.1286772234568,
20.8532334758975));
#204127=CARTESIAN_POINT('Ctrl Pts',(-19.6380869386121,21.1252455705182,
20.852746362086));
#204128=CARTESIAN_POINT('Ctrl Pts',(-19.6421586496785,21.1233172238658,
20.8524752965508));
#204129=CARTESIAN_POINT('Ctrl Pts',(-19.6544483063059,21.1174487858528,
20.851658265905));
#204130=CARTESIAN_POINT('Ctrl Pts',(-19.6626471178375,21.1134685529421,
20.8511147275499));
#204131=CARTESIAN_POINT('Ctrl Pts',(-19.7255937342003,21.0824063123546,
20.8469515638468));
#204132=CARTESIAN_POINT('Ctrl Pts',(-19.7791774679564,21.053016625207,20.8434651113395));
#204133=CARTESIAN_POINT('Ctrl Pts',(-19.970858594242,20.9368208952867,20.830935854194));
#204134=CARTESIAN_POINT('Ctrl Pts',(-20.1000689129344,20.8364655914837,
20.822334830644));
#204135=CARTESIAN_POINT('Ctrl Pts',(-20.273107884421,20.6667223149079,20.8088862894272));
#204136=CARTESIAN_POINT('Ctrl Pts',(-20.326559848166,20.6080439164103,20.8043989788281));
#204137=CARTESIAN_POINT('Ctrl Pts',(-20.3888156628394,20.5314732708347,
20.7986403352534));
#204138=CARTESIAN_POINT('Ctrl Pts',(-20.4008334149378,20.516270419079,20.7975016064567));
#204139=CARTESIAN_POINT('Ctrl Pts',(-20.4179162143748,20.4940394201979,
20.7958420496877));
#204140=CARTESIAN_POINT('Ctrl Pts',(-20.4231497182485,20.4871415269321,
20.7953278842124));
#204141=CARTESIAN_POINT('Ctrl Pts',(-20.4322172523282,20.4750367765264,
20.7944268409866));
#204142=CARTESIAN_POINT('Ctrl Pts',(-20.4360700412672,20.4698440656832,
20.794040704147));
#204143=CARTESIAN_POINT('Ctrl Pts',(-20.44348071136,20.4597598975513,20.7932915529837));
#204144=CARTESIAN_POINT('Ctrl Pts',(-20.4470415409671,20.4548706773554,
20.7929286584954));
#204145=CARTESIAN_POINT('Ctrl Pts',(-20.4554657132141,20.4431990307194,
20.7920630847887));
#204146=CARTESIAN_POINT('Ctrl Pts',(-20.4603099695392,20.436403010861,20.7915596757553));
#204147=CARTESIAN_POINT('Ctrl Pts',(-20.47743454376,20.4120758252375,20.7897596208191));
#204148=CARTESIAN_POINT('Ctrl Pts',(-20.4894886989085,20.3943877308616,
20.7884543995981));
#204149=CARTESIAN_POINT('Ctrl Pts',(-20.5919348107623,20.239049248216,20.7770190655048));
#204150=CARTESIAN_POINT('Ctrl Pts',(-20.666182344048,20.0915668540658,20.7662793195637));
#204151=CARTESIAN_POINT('Ctrl Pts',(-20.7225806115197,19.937110288791,20.7554137119617));
#204152=CARTESIAN_POINT('',(-20.8509997094729,19.2098909049546,21.2890562789773));
#204153=CARTESIAN_POINT('Ctrl Pts',(-20.8509997094729,19.2098909049547,
21.2890562789773));
#204154=CARTESIAN_POINT('Ctrl Pts',(-20.8509573536458,19.1290436646228,
21.2842160160334));
#204155=CARTESIAN_POINT('Ctrl Pts',(-20.8462795755055,19.0483584782395,
21.2793757530895));
#204156=CARTESIAN_POINT('Ctrl Pts',(-20.837046582522,18.9683395958493,21.2745354901457));
#204157=CARTESIAN_POINT('Ctrl Pts',(-20.8277795400084,18.8880256189704,
21.2696773772284));
#204158=CARTESIAN_POINT('Ctrl Pts',(-20.8139237586678,18.8083831470337,
21.2648192643112));
#204159=CARTESIAN_POINT('Ctrl Pts',(-20.795610244073,18.7299052052522,21.259961151394));
#204160=CARTESIAN_POINT('Ctrl Pts',(-20.7772066847249,18.6510413994209,
21.2550791518778));
#204161=CARTESIAN_POINT('Ctrl Pts',(-20.7543015879878,18.5733538729021,
21.2501971523617));
#204162=CARTESIAN_POINT('Ctrl Pts',(-20.7270761473527,18.4973218716721,
21.2453151528455));
#204163=CARTESIAN_POINT('Ctrl Pts',(-20.7141466883093,18.4612140025996,
21.2429966738302));
#204164=CARTESIAN_POINT('Ctrl Pts',(-20.7002435345946,18.4254791783653,
21.2406781948149));
#204165=CARTESIAN_POINT('Ctrl Pts',(-20.6853897306834,18.3901668141557,
21.2383597157996));
#204166=CARTESIAN_POINT('Ctrl Pts',(-20.6572744298791,18.3233275218235,
21.2339712954789));
#204167=CARTESIAN_POINT('Ctrl Pts',(-20.6256662319327,18.2578040404403,
21.2295828751582));
#204168=CARTESIAN_POINT('Ctrl Pts',(-20.5907099296459,18.1939861175213,
21.2251944548374));
#204169=CARTESIAN_POINT('Ctrl Pts',(-20.555805493452,18.1302628838601,21.2208125457951));
#204170=CARTESIAN_POINT('Ctrl Pts',(-20.5175630443477,18.0682406045754,
21.2164306367528));
#204171=CARTESIAN_POINT('Ctrl Pts',(-20.4761752802482,18.0082887741057,
21.2120487277105));
#204172=CARTESIAN_POINT('Ctrl Pts',(-20.4348361356984,17.9484073709969,
21.207671966239));
#204173=CARTESIAN_POINT('Ctrl Pts',(-20.3903592887853,17.8905919800195,
21.2032952047674));
#204174=CARTESIAN_POINT('Ctrl Pts',(-20.3429823042688,17.8351857158214,
21.1989184432959));
#204175=CARTESIAN_POINT('Ctrl Pts',(-20.2956353568299,17.779814579276,21.1945444566975));
#204176=CARTESIAN_POINT('Ctrl Pts',(-20.2453922326902,17.7268499046386,
21.1901704700991));
#204177=CARTESIAN_POINT('Ctrl Pts',(-20.1925317242827,17.6766029818652,
21.1857964835008));
#204178=CARTESIAN_POINT('Ctrl Pts',(-20.1396872964519,17.6263713445954,
21.181423827503));
#204179=CARTESIAN_POINT('Ctrl Pts',(-20.084227414496,17.5788561499108,21.1770511715053));
#204180=CARTESIAN_POINT('Ctrl Pts',(-20.0264676125179,17.5343317350793,
21.1726785155076));
#204181=CARTESIAN_POINT('Ctrl Pts',(-19.9687063332045,17.4898061814369,
21.1683057476695));
#204182=CARTESIAN_POINT('Ctrl Pts',(-19.9086454002984,17.4482718524075,
21.1639329798313));
#204183=CARTESIAN_POINT('Ctrl Pts',(-19.8466319557782,17.409961651996,21.1595602119932));
#204184=CARTESIAN_POINT('Ctrl Pts',(-19.7845541750513,17.3716117064453,
21.1551829076018));
#204185=CARTESIAN_POINT('Ctrl Pts',(-19.7205202495877,17.3364928218529,
21.1508056032104));
#204186=CARTESIAN_POINT('Ctrl Pts',(-19.6549040128954,17.3047930859864,
21.1464282988189));
#204187=CARTESIAN_POINT('Ctrl Pts',(-19.5892519496617,17.2730760420274,
21.1420486044142));
#204188=CARTESIAN_POINT('Ctrl Pts',(-19.5220162999603,17.2447820509217,
21.1376689100095));
#204189=CARTESIAN_POINT('Ctrl Pts',(-19.4535905649465,17.220050874874,21.1332892156048));
#204190=CARTESIAN_POINT('Ctrl Pts',(-19.3850436009877,17.1952758829377,
21.1289017617551));
#204191=CARTESIAN_POINT('Ctrl Pts',(-19.3153028030891,17.1740764516624,
21.1245143079053));
#204192=CARTESIAN_POINT('Ctrl Pts',(-19.2447759299221,17.1565421762878,
21.1201268540555));
#204193=CARTESIAN_POINT('Ctrl Pts',(-19.196857633423,17.1446288081125,21.1171458724097));
#204194=CARTESIAN_POINT('Ctrl Pts',(-19.1485767107386,17.13440631873,21.1141648907639));
#204195=CARTESIAN_POINT('Ctrl Pts',(-19.1000625458484,17.1258891606135,
21.111183909118));
#204196=CARTESIAN_POINT('Ctrl Pts',(-19.0286448054896,17.1133510454397,
21.1067956036885));
#204197=CARTESIAN_POINT('Ctrl Pts',(-18.9564428209882,17.1044619390322,
21.102407298259));
#204198=CARTESIAN_POINT('Ctrl Pts',(-18.8838626628663,17.0993110592991,
21.0980189928294));
#204199=CARTESIAN_POINT('Ctrl Pts',(-18.8113901833097,17.0941678213148,
21.0936371978078));
#204200=CARTESIAN_POINT('Ctrl Pts',(-18.7385411210672,17.0927518343552,
21.0892554027861));
#204201=CARTESIAN_POINT('Ctrl Pts',(-18.6657304479849,17.0951010732392,
21.0848736077645));
#204202=CARTESIAN_POINT('Ctrl Pts',(-18.593005279013,17.09744755333,21.0804969584374));
#204203=CARTESIAN_POINT('Ctrl Pts',(-18.5203188893578,17.1035504601723,
21.0761203091104));
#204204=CARTESIAN_POINT('Ctrl Pts',(-18.4480883559106,17.1133957637881,
21.0717436597833));
#204205=CARTESIAN_POINT('Ctrl Pts',(-18.3759035978361,17.123234828042,21.0673697841136));
#204206=CARTESIAN_POINT('Ctrl Pts',(-18.3041745995243,17.1368115183043,
21.0629959084439));
#204207=CARTESIAN_POINT('Ctrl Pts',(-18.2333139941715,17.1540599124993,
21.0586220327743));
#204208=CARTESIAN_POINT('Ctrl Pts',(-18.1624749233001,17.171303064921,21.0542494863219));
#204209=CARTESIAN_POINT('Ctrl Pts',(-18.0925041898433,17.192215591997,21.0498769398696));
#204210=CARTESIAN_POINT('Ctrl Pts',(-18.0238032429013,17.2166806759683,
21.0455043934172));
#204211=CARTESIAN_POINT('Ctrl Pts',(-17.955100514348,17.2411463943888,21.0411317335723));
#204212=CARTESIAN_POINT('Ctrl Pts',(-17.8876680914168,17.269164688916,21.0367590737273));
#204213=CARTESIAN_POINT('Ctrl Pts',(-17.8218896924817,17.3005697377504,
21.0323864138824));
#204214=CARTESIAN_POINT('Ctrl Pts',(-17.7560430020855,17.3320073914629,
21.0280092143203));
#204215=CARTESIAN_POINT('Ctrl Pts',(-17.691854200438,17.3668386114322,21.0236320147581));
#204216=CARTESIAN_POINT('Ctrl Pts',(-17.6296837695453,17.404850874608,21.019254815196));
#204217=CARTESIAN_POINT('Ctrl Pts',(-17.567479369866,17.4428839069893,21.0148752240121));
#204218=CARTESIAN_POINT('Ctrl Pts',(-17.5072959348518,17.4841011703041,
21.0104956328281));
#204219=CARTESIAN_POINT('Ctrl Pts',(-17.4494639567956,17.5282474472731,
21.0061160416442));
#204220=CARTESIAN_POINT('Ctrl Pts',(-17.3915294664699,17.5724719774023,
21.0017286872495));
#204221=CARTESIAN_POINT('Ctrl Pts',(-17.3359551248471,17.6196355768842,
20.9973413328549));
#204222=CARTESIAN_POINT('Ctrl Pts',(-17.2830369579979,17.6694438866055,
20.9929539784602));
#204223=CARTESIAN_POINT('Ctrl Pts',(-17.2470700010395,17.703297163062,20.9899720197857));
#204224=CARTESIAN_POINT('Ctrl Pts',(-17.2123293114184,17.738371385165,20.9869900611112));
#204225=CARTESIAN_POINT('Ctrl Pts',(-17.1788971521192,17.7745654792115,
20.9840081024367));
#204226=CARTESIAN_POINT('Ctrl Pts',(-17.1297000971194,17.8278268560652,
20.9796200046294));
#204227=CARTESIAN_POINT('Ctrl Pts',(-17.0831463841702,17.8837226314485,
20.975231906822));
#204228=CARTESIAN_POINT('Ctrl Pts',(-17.0395308345184,17.941959714102,20.9708438090147));
#204229=CARTESIAN_POINT('Ctrl Pts',(-16.9959800368753,18.000110337497,20.9664622258139));
#204230=CARTESIAN_POINT('Ctrl Pts',(-16.9553590301246,18.0605949850623,
20.9620806426132));
#204231=CARTESIAN_POINT('Ctrl Pts',(-16.9179243707118,18.1230853394197,
20.9576990594124));
#204232=CARTESIAN_POINT('Ctrl Pts',(-16.8805337191531,18.1855022306699,
20.9533226271621));
#204233=CARTESIAN_POINT('Ctrl Pts',(-16.8463222204768,18.2499197329738,
20.9489461949117));
#204234=CARTESIAN_POINT('Ctrl Pts',(-16.8155038458629,18.3159796055054,
20.9445697626614));
#204235=CARTESIAN_POINT('Ctrl Pts',(-16.7847050250506,18.3819975640277,
20.9401961071924));
#204236=CARTESIAN_POINT('Ctrl Pts',(-16.7572952601506,18.4496553891047,
20.9358224517234));
#204237=CARTESIAN_POINT('Ctrl Pts',(-16.7334424864511,18.5185704837437,
20.9314487962544));
#204238=CARTESIAN_POINT('Ctrl Pts',(-16.709596977258,18.5874645898738,20.9270764728086));
#204239=CARTESIAN_POINT('Ctrl Pts',(-16.68930646627,18.6576147497773,20.9227041493628));
#204240=CARTESIAN_POINT('Ctrl Pts',(-16.6726900413674,18.7286202176274,
20.918331825917));
#204241=CARTESIAN_POINT('Ctrl Pts',(-16.6560731949978,18.7996274864939,
20.9139593915695));
#204242=CARTESIAN_POINT('Ctrl Pts',(-16.6431307277095,18.8714896362078,
20.9095869572221));
#204243=CARTESIAN_POINT('Ctrl Pts',(-16.6339309262445,18.9437943012289,
20.9052145228746));
#204244=CARTESIAN_POINT('Ctrl Pts',(-16.6247215778304,19.0161739992776,
20.9008375511022));
#204245=CARTESIAN_POINT('Ctrl Pts',(-16.6192627107137,19.0889966499121,
20.8964605793299));
#204246=CARTESIAN_POINT('Ctrl Pts',(-16.617570766158,19.1618441444085,20.8920836075575));
#204247=CARTESIAN_POINT('Ctrl Pts',(-16.6158778977392,19.23473141628,20.8877042457998));
#204248=CARTESIAN_POINT('Ctrl Pts',(-16.6179560333427,19.307643076478,20.883324884042));
#204249=CARTESIAN_POINT('Ctrl Pts',(-16.6237694821509,19.3801631210935,
20.8789455222842));
#204250=CARTESIAN_POINT('Ctrl Pts',(-16.6295932362114,19.4528117188942,
20.874558397419));
#204251=CARTESIAN_POINT('Ctrl Pts',(-16.6391654627898,19.5250668361741,
20.8701712725537));
#204252=CARTESIAN_POINT('Ctrl Pts',(-16.6523989027095,19.5965202611523,
20.8657841476884));
#204253=CARTESIAN_POINT('Ctrl Pts',(-16.6613997706558,19.645120084512,20.862800197044));
#204254=CARTESIAN_POINT('Ctrl Pts',(-16.6720933116133,19.6933492436894,
20.8598162463996));
#204255=CARTESIAN_POINT('Ctrl Pts',(-16.684438979983,19.741083602111,20.8568322957552));
#204256=CARTESIAN_POINT('Ctrl Pts',(-16.702594716654,19.8112825104007,20.852444050379));
#204257=CARTESIAN_POINT('Ctrl Pts',(-16.7243966034831,19.8806845781119,
20.8480558050029));
#204258=CARTESIAN_POINT('Ctrl Pts',(-16.749757746659,19.9488832428347,20.8436675596267));
#204259=CARTESIAN_POINT('Ctrl Pts',(-16.7750812520095,20.0169806956596,
20.8392858267335));
#204260=CARTESIAN_POINT('Ctrl Pts',(-16.8039533610691,20.0838778424496,
20.8349040938403));
#204261=CARTESIAN_POINT('Ctrl Pts',(-16.8362368493152,20.1491812319072,
20.8305223609472));
#204262=CARTESIAN_POINT('Ctrl Pts',(-16.868482404701,20.2144078903644,20.8261457765578));
#204263=CARTESIAN_POINT('Ctrl Pts',(-16.9041311639573,20.2780440812599,
20.8217691921684));
#204264=CARTESIAN_POINT('Ctrl Pts',(-16.9429976922085,20.3397159667008,
20.817392607779));
#204265=CARTESIAN_POINT('Ctrl Pts',(-16.9818395737555,20.4013487437166,
20.8130187987438));
#204266=CARTESIAN_POINT('Ctrl Pts',(-17.0238949191149,20.4610192797036,
20.8086449897085));
#204267=CARTESIAN_POINT('Ctrl Pts',(-17.0689328967322,20.5183792646418,
20.8042711806733));
#204268=CARTESIAN_POINT('Ctrl Pts',(-17.1139571706356,20.5757217966466,
20.7998987024578));
#204269=CARTESIAN_POINT('Ctrl Pts',(-17.1619619773634,20.6307547941729,
20.7955262242422));
#204270=CARTESIAN_POINT('Ctrl Pts',(-17.212674786275,20.6831611984034,20.7911537460267));
#204271=CARTESIAN_POINT('Ctrl Pts',(-17.2633888928252,20.7355689436083,
20.7867811559282));
#204272=CARTESIAN_POINT('Ctrl Pts',(-17.3168108022569,20.7853496168292,
20.7824085658297));
#204273=CARTESIAN_POINT('Ctrl Pts',(-17.3726307171725,20.8322225867455,
20.7780359757313));
#204274=CARTESIAN_POINT('Ctrl Pts',(-17.4285085618265,20.8791442012878,
20.7736588477721));
#204275=CARTESIAN_POINT('Ctrl Pts',(-17.4867890105141,20.9231517768141,
20.7692817198129));
#204276=CARTESIAN_POINT('Ctrl Pts',(-17.5471293748475,20.9640051680329,
20.7649045918536));
#204277=CARTESIAN_POINT('Ctrl Pts',(-17.6075026927368,21.0048808704282,
20.7605250734228));
#204278=CARTESIAN_POINT('Ctrl Pts',(-17.6699377529298,21.0425987092605,
20.7561455549919));
#204279=CARTESIAN_POINT('Ctrl Pts',(-17.7340654194772,21.0769635137576,
20.751766036561));
#204280=CARTESIAN_POINT('Ctrl Pts',(-17.7983067443387,21.1113892255971,
20.7473787559784));
#204281=CARTESIAN_POINT('Ctrl Pts',(-17.8642462295391,21.1424498297606,
20.7429914753957));
#204282=CARTESIAN_POINT('Ctrl Pts',(-17.931493378709,21.1699977342468,20.738604194813));
#204283=CARTESIAN_POINT('Ctrl Pts',(-17.9772094505245,21.18872539773,20.7356216262333));
#204284=CARTESIAN_POINT('Ctrl Pts',(-18.023529468233,21.2058306584364,20.7326390576535));
#204285=CARTESIAN_POINT('Ctrl Pts',(-18.0703272881618,21.2212804609212,
20.7296564890738));
#204286=CARTESIAN_POINT('Ctrl Pts',(-18.1391803751011,21.2440115752187,
20.7252682706902));
#204287=CARTESIAN_POINT('Ctrl Pts',(-18.2093370327966,21.2632455876901,
20.7208800523066));
#204288=CARTESIAN_POINT('Ctrl Pts',(-18.2804083778876,21.278835496443,20.716491833923));
#204289=CARTESIAN_POINT('Ctrl Pts',(-18.3513742461451,21.2944022682451,
20.7121101280851));
#204290=CARTESIAN_POINT('Ctrl Pts',(-18.423251639725,21.3063355698589,20.7077284222471));
#204291=CARTESIAN_POINT('Ctrl Pts',(-18.4956354561782,21.3145378162155,
20.7033467164092));
#204292=CARTESIAN_POINT('Ctrl Pts',(-18.5679342223251,21.3227304250094,
20.6989701590346));
#204293=CARTESIAN_POINT('Ctrl Pts',(-18.6407377523612,21.3272006332577,
20.6945936016599));
#204294=CARTESIAN_POINT('Ctrl Pts',(-18.7136313399141,21.3279020094672,
20.6902170442853));
#204295=CARTESIAN_POINT('Ctrl Pts',(-18.7864787033138,21.3286029409117,
20.6858432622256));
#204296=CARTESIAN_POINT('Ctrl Pts',(-18.8594155297534,21.325539777633,20.6814694801658));
#204297=CARTESIAN_POINT('Ctrl Pts',(-18.9320240051558,21.3187180773011,
20.6770956981061));
#204298=CARTESIAN_POINT('Ctrl Pts',(-19.0046103891442,21.3118984524984,
20.6727232467868));
#204299=CARTESIAN_POINT('Ctrl Pts',(-19.0768681404601,21.3013226060357,
20.6683507954674));
#204300=CARTESIAN_POINT('Ctrl Pts',(-19.1483831512649,21.2870480736119,
20.663978344148));
#204301=CARTESIAN_POINT('Ctrl Pts',(-19.2198999939593,21.2727731755395,
20.6596057808264));
#204302=CARTESIAN_POINT('Ctrl Pts',(-19.2906735857164,21.2547994997832,
20.6552332175047));
#204303=CARTESIAN_POINT('Ctrl Pts',(-19.3603002766085,21.2332356350139,
20.650860654183));
#204304=CARTESIAN_POINT('Ctrl Pts',(-19.4299992322408,21.2116493893579,
20.6464835526282));
#204305=CARTESIAN_POINT('Ctrl Pts',(-19.4985484486157,21.1864656580614,
20.6421064510734));
#204306=CARTESIAN_POINT('Ctrl Pts',(-19.5655605148557,21.1578426002461,
20.6377293495187));
#204307=CARTESIAN_POINT('Ctrl Pts',(-19.6326091810389,21.1292039093911,
20.6333498573247));
#204308=CARTESIAN_POINT('Ctrl Pts',(-19.6981185920468,21.0971223643352,
20.6289703651308));
#204309=CARTESIAN_POINT('Ctrl Pts',(-19.761724838013,21.0618027062146,20.6245908729369));
#204310=CARTESIAN_POINT('Ctrl Pts',(-19.8254438270173,21.0264204434629,
20.6202036180265));
#204311=CARTESIAN_POINT('Ctrl Pts',(-19.8872525050491,20.9877888617786,
20.6158163631161));
#204312=CARTESIAN_POINT('Ctrl Pts',(-19.9468154065796,20.9461564164545,
20.6114291082057));
#204313=CARTESIAN_POINT('Ctrl Pts',(-19.9873110556401,20.9178513330544,
20.6084462996012));
#204314=CARTESIAN_POINT('Ctrl Pts',(-20.0267692618289,20.8881600264952,
20.6054634909968));
#204315=CARTESIAN_POINT('Ctrl Pts',(-20.065093928451,20.8571706939564,20.6024806823923));
#204316=CARTESIAN_POINT('Ctrl Pts',(-20.1207334286554,20.8121805837716,
20.59815026038));
#204317=CARTESIAN_POINT('Ctrl Pts',(-20.1742116960449,20.7642672661332,
20.5938198383676));
#204318=CARTESIAN_POINT('Ctrl Pts',(-20.2251992661504,20.7136688752458,
20.5894894163552));
#204319=CARTESIAN_POINT('Ctrl Pts',(-20.2761150699366,20.6631417028979,
20.5851650895235));
#204320=CARTESIAN_POINT('Ctrl Pts',(-20.3245467786866,20.6099372970267,
20.5808407626917));
#204321=CARTESIAN_POINT('Ctrl Pts',(-20.3701971565707,20.5543346064291,
20.57651643586));
#204322=CARTESIAN_POINT('Ctrl Pts',(-20.4157961637033,20.4987944860036,
20.5721969752293));
#204323=CARTESIAN_POINT('Ctrl Pts',(-20.4586197391826,20.4408618191658,
20.5678775145986));
#204324=CARTESIAN_POINT('Ctrl Pts',(-20.498408153215,20.3808516439567,20.563558053968));
#204325=CARTESIAN_POINT('Ctrl Pts',(-20.5381709780786,20.3208800631614,
20.5592413713171));
#204326=CARTESIAN_POINT('Ctrl Pts',(-20.5749022411959,20.2588340376598,
20.5549246886661));
#204327=CARTESIAN_POINT('Ctrl Pts',(-20.6083841486135,20.1950594816507,
20.5506080060152));
#204328=CARTESIAN_POINT('Ctrl Pts',(-20.6418605361497,20.1312954396179,
20.5462920350196));
#204329=CARTESIAN_POINT('Ctrl Pts',(-20.6720883966209,20.0658038696194,
20.5419760640239));
#204330=CARTESIAN_POINT('Ctrl Pts',(-20.6988955814925,19.9989558070293,
20.5376600930283));
#204331=CARTESIAN_POINT('Ctrl Pts',(-20.7071130320822,19.978464261424,20.5363370791209));
#204332=CARTESIAN_POINT('Ctrl Pts',(-20.7150093912817,19.9578454053111,
20.5350140652135));
#204333=CARTESIAN_POINT('Ctrl Pts',(-20.7225806064498,19.9371103026755,
20.5336910513061));
#204334=CARTESIAN_POINT('Ctrl Pts',(-20.7225806064498,19.9371103026755,
21.3335535417785));
#204335=CARTESIAN_POINT('Ctrl Pts',(-20.7478890194195,19.8677987682902,
21.3291191901433));
#204336=CARTESIAN_POINT('Ctrl Pts',(-20.7695971958024,19.7970870004519,
21.324684838508));
#204337=CARTESIAN_POINT('Ctrl Pts',(-20.7875591110991,19.725377271292,21.3202504868728));
#204338=CARTESIAN_POINT('Ctrl Pts',(-20.8055066416424,19.6537249706835,
21.3158196864766));
#204339=CARTESIAN_POINT('Ctrl Pts',(-20.8197137585767,19.5810767457616,
21.3113888860803));
#204340=CARTESIAN_POINT('Ctrl Pts',(-20.8300842035801,19.5078501499109,
21.3069580856841));
#204341=CARTESIAN_POINT('Ctrl Pts',(-20.8404495509225,19.4346595490787,
21.3025294632772));
#204342=CARTESIAN_POINT('Ctrl Pts',(-20.8469819090597,19.360891601732,21.2981008408703));
#204343=CARTESIAN_POINT('Ctrl Pts',(-20.8496363437061,19.2869727661079,
21.2936722184634));
#204344=CARTESIAN_POINT('Ctrl Pts',(-20.8505585800474,19.2612909748395,
21.2921335719831));
#204345=CARTESIAN_POINT('Ctrl Pts',(-20.8510131737418,19.2355910222583,
21.2905949255028));
#204346=CARTESIAN_POINT('Ctrl Pts',(-20.8509997094733,19.2098909057104,
21.2890562790225));
#204347=CARTESIAN_POINT('Origin',(-18.734,19.211,0.));
#204348=CARTESIAN_POINT('',(-20.3539402646795,17.8481050888384,21.9999997807644));
#204349=CARTESIAN_POINT('Ctrl Pts',(-20.3539402646795,17.8481050888384,
21.9999997807644));
#204350=CARTESIAN_POINT('Ctrl Pts',(-20.3072934957001,17.7926606237751,
21.9956147707751));
#204351=CARTESIAN_POINT('Ctrl Pts',(-20.2577053013778,17.7395048193498,
21.9912297607858));
#204352=CARTESIAN_POINT('Ctrl Pts',(-20.2054290597327,17.6889666487971,
21.9868447507965));
#204353=CARTESIAN_POINT('Ctrl Pts',(-20.1532304392223,17.6385035186453,
21.982466251785));
#204354=CARTESIAN_POINT('Ctrl Pts',(-20.0983520388586,17.5906506399773,
21.9780877527736));
#204355=CARTESIAN_POINT('Ctrl Pts',(-20.0410869968869,17.545703455066,21.9737092537621));
#204356=CARTESIAN_POINT('Ctrl Pts',(-19.9838893502852,17.5008091686081,
21.969335907817));
#204357=CARTESIAN_POINT('Ctrl Pts',(-19.9243110199867,17.4588140795273,
21.9649625618719));
#204358=CARTESIAN_POINT('Ctrl Pts',(-19.8626801771137,17.4199751375844,
21.9605892159267));
#204359=CARTESIAN_POINT('Ctrl Pts',(-19.8010883319371,17.381160771474,21.9562186372717));
#204360=CARTESIAN_POINT('Ctrl Pts',(-19.7374469588082,17.3454988470316,
21.9518480586166));
#204361=CARTESIAN_POINT('Ctrl Pts',(-19.6721141643387,17.3132036951593,
21.9474774799615));
#204362=CARTESIAN_POINT('Ctrl Pts',(-19.6068010732891,17.2809182830347,
21.9431082194094));
#204363=CARTESIAN_POINT('Ctrl Pts',(-19.539798006527,17.2519978415642,21.9387389588572));
#204364=CARTESIAN_POINT('Ctrl Pts',(-19.4714871908732,17.2266105111904,
21.934369698305));
#204365=CARTESIAN_POINT('Ctrl Pts',(-19.4031743543433,17.2012224297694,
21.9300003084946));
#204366=CARTESIAN_POINT('Ctrl Pts',(-19.33355414576,17.1793678332055,21.9256309186843));
#204367=CARTESIAN_POINT('Ctrl Pts',(-19.2630266691229,17.1611659132123,
21.9212615288739));
#204368=CARTESIAN_POINT('Ctrl Pts',(-19.1924273973489,17.142945464138,21.9168876911383));
#204369=CARTESIAN_POINT('Ctrl Pts',(-19.1209194825959,17.1283852352836,
21.9125138534028));
#204370=CARTESIAN_POINT('Ctrl Pts',(-19.0489151638194,17.1175536931661,
21.9081400156672));
#204371=CARTESIAN_POINT('Ctrl Pts',(-18.9768710224476,17.1067161605729,
21.9037637589438));
#204372=CARTESIAN_POINT('Ctrl Pts',(-18.9043304115686,17.0996114670891,
21.8993875022204));
#204373=CARTESIAN_POINT('Ctrl Pts',(-18.8317099769259,17.096256100515,21.895011245497));
#204374=CARTESIAN_POINT('Ctrl Pts',(-18.7589654023404,17.0928949981583,
21.8906275078454));
#204375=CARTESIAN_POINT('Ctrl Pts',(-18.6861412147951,17.0932960158796,
21.8862437701938));
#204376=CARTESIAN_POINT('Ctrl Pts',(-18.6136526546588,17.0974235248117,
21.8818600325422));
#204377=CARTESIAN_POINT('Ctrl Pts',(-18.5716446773508,17.099815465019,21.8793196047637));
#204378=CARTESIAN_POINT('Ctrl Pts',(-18.5297493105789,17.1034579173405,
21.8767791769852));
#204379=CARTESIAN_POINT('Ctrl Pts',(-18.4880458594114,17.1083360799388,
21.8742387492067));
#204380=CARTESIAN_POINT('Ctrl Pts',(-18.4158852200683,17.116776900112,21.8698429764932));
#204381=CARTESIAN_POINT('Ctrl Pts',(-18.3440242584073,17.1289525208195,
21.8654472037797));
#204382=CARTESIAN_POINT('Ctrl Pts',(-18.272878821027,17.1448305349506,21.8610514310662));
#204383=CARTESIAN_POINT('Ctrl Pts',(-18.2018362105903,17.160685600489,21.8566620115904));
#204384=CARTESIAN_POINT('Ctrl Pts',(-18.1315075364803,17.1802323315536,
21.8522725921145));
#204385=CARTESIAN_POINT('Ctrl Pts',(-18.0623022824371,17.2033866965422,
21.8478831726387));
#204386=CARTESIAN_POINT('Ctrl Pts',(-17.9931750463637,17.2265149586492,
21.8434987015386));
#204387=CARTESIAN_POINT('Ctrl Pts',(-17.9251691678202,17.2532426232453,
21.8391142304384));
#204388=CARTESIAN_POINT('Ctrl Pts',(-17.8586810826102,17.2834352688276,
21.8347297593383));
#204389=CARTESIAN_POINT('Ctrl Pts',(-17.7922332814893,17.3136096211591,
21.8303479447205));
#204390=CARTESIAN_POINT('Ctrl Pts',(-17.7273018852858,17.3472445902797,
21.8259661301027));
#204391=CARTESIAN_POINT('Ctrl Pts',(-17.6642640529712,17.384157367578,21.8215843154849));
#204392=CARTESIAN_POINT('Ctrl Pts',(-17.601243827434,17.4210598349556,21.8172037247295));
#204393=CARTESIAN_POINT('Ctrl Pts',(-17.5401165299889,17.4612380500253,
21.8128231339742));
#204394=CARTESIAN_POINT('Ctrl Pts',(-17.4812339028314,17.5044637109674,
21.8084425432188));
#204395=CARTESIAN_POINT('Ctrl Pts',(-17.4223484927206,17.547691414872,21.8040617454248));
#204396=CARTESIAN_POINT('Ctrl Pts',(-17.365708349646,17.5939665647424,21.7996809476307));
#204397=CARTESIAN_POINT('Ctrl Pts',(-17.3116341001189,17.6430190540522,
21.7953001498367));
#204398=CARTESIAN_POINT('Ctrl Pts',(-17.2575027316979,17.692123357746,21.7909147245846));
#204399=CARTESIAN_POINT('Ctrl Pts',(-17.2059430246541,17.7440105345835,
21.7865292993325));
#204400=CARTESIAN_POINT('Ctrl Pts',(-17.1572399043858,17.798372447926,21.7821438740803));
#204401=CARTESIAN_POINT('Ctrl Pts',(-17.1085095392263,17.852764771731,21.7777559955884));
#204402=CARTESIAN_POINT('Ctrl Pts',(-17.0626392444271,17.9096342143152,
21.7733681170964));
#204403=CARTESIAN_POINT('Ctrl Pts',(-17.0198729444951,17.9686403750982,
21.7689802386045));
#204404=CARTESIAN_POINT('Ctrl Pts',(-16.9770309082245,18.0277510319582,
21.7645845894648));
#204405=CARTESIAN_POINT('Ctrl Pts',(-16.9373041057529,18.0890055601327,
21.7601889403251));
#204406=CARTESIAN_POINT('Ctrl Pts',(-16.9008922045882,18.1520359730375,
21.7557932911855));
#204407=CARTESIAN_POINT('Ctrl Pts',(-16.8767858983712,18.1937649238989,
21.7528831749654));
#204408=CARTESIAN_POINT('Ctrl Pts',(-16.8541315758308,18.2362717295104,
21.7499730587453));
#204409=CARTESIAN_POINT('Ctrl Pts',(-16.8329755513189,18.2794448242231,
21.7470629425252));
#204410=CARTESIAN_POINT('Ctrl Pts',(-16.8011149074337,18.3444628334097,
21.7426803527574));
#204411=CARTESIAN_POINT('Ctrl Pts',(-16.772529978103,18.4112473176336,21.7382977629896));
#204412=CARTESIAN_POINT('Ctrl Pts',(-16.7474198249775,18.4794344129146,
21.7339151732219));
#204413=CARTESIAN_POINT('Ctrl Pts',(-16.7223474511024,18.5475189179272,
21.7295391772393));
#204414=CARTESIAN_POINT('Ctrl Pts',(-16.7007396419766,18.6170013950868,
21.7251631812567));
#204415=CARTESIAN_POINT('Ctrl Pts',(-16.6827487806458,18.6874950476855,
21.7207871852741));
#204416=CARTESIAN_POINT('Ctrl Pts',(-16.6647794728902,18.7579042468375,
21.7164164318621));
#204417=CARTESIAN_POINT('Ctrl Pts',(-16.650418624554,18.8293217487381,21.71204567845));
#204418=CARTESIAN_POINT('Ctrl Pts',(-16.6397692918518,18.9013441570891,
21.7076749250379));
#204419=CARTESIAN_POINT('Ctrl Pts',(-16.6291268554032,18.973319925447,21.7033070020215));
#204420=CARTESIAN_POINT('Ctrl Pts',(-16.6221912368165,19.0458993457387,
21.698939079005));
#204421=CARTESIAN_POINT('Ctrl Pts',(-16.6190144349639,19.1186687502037,
21.6945711559885));
#204422=CARTESIAN_POINT('Ctrl Pts',(-16.6158386349475,19.19141520611,21.6902046104402));
#204423=CARTESIAN_POINT('Ctrl Pts',(-16.6164193196609,19.2643510442235,
21.6858380648919));
#204424=CARTESIAN_POINT('Ctrl Pts',(-16.6207564965869,19.3370590944058,
21.6814715193436));
#204425=CARTESIAN_POINT('Ctrl Pts',(-16.6250937465921,19.4097683696811,
21.6771049002213));
#204426=CARTESIAN_POINT('Ctrl Pts',(-16.6331875836567,19.4822493665785,
21.6727382810989));
#204427=CARTESIAN_POINT('Ctrl Pts',(-16.6449860089037,19.5540882466713,
21.6683716619766));
#204428=CARTESIAN_POINT('Ctrl Pts',(-16.6567966463011,19.6260014847561,
21.6640005231147));
#204429=CARTESIAN_POINT('Ctrl Pts',(-16.6723194491993,19.6972708005986,
21.6596293842528));
#204430=CARTESIAN_POINT('Ctrl Pts',(-16.6914510872628,19.7674916343271,
21.6552582453909));
#204431=CARTESIAN_POINT('Ctrl Pts',(-16.7105931022024,19.8377505553794,
21.6508847356516));
#204432=CARTESIAN_POINT('Ctrl Pts',(-16.7333476979536,19.9069594022358,
21.6465112259124));
#204433=CARTESIAN_POINT('Ctrl Pts',(-16.7595621821267,19.9747305174941,
21.6421377161732));
#204434=CARTESIAN_POINT('Ctrl Pts',(-16.7858234022015,20.0426224569562,
21.6377564092208));
#204435=CARTESIAN_POINT('Ctrl Pts',(-16.8155566307479,20.1090711042367,
21.6333751022684));
#204436=CARTESIAN_POINT('Ctrl Pts',(-16.8485619796008,20.1737110008893,
21.6289937953161));
#204437=CARTESIAN_POINT('Ctrl Pts',(-16.8714294691446,20.2184962315317,
21.6259582421587));
#204438=CARTESIAN_POINT('Ctrl Pts',(-16.8958666987907,20.2624137158362,
21.6229226890013));
#204439=CARTESIAN_POINT('Ctrl Pts',(-16.9217951496002,20.3053503004923,
21.6198871358439));
#204440=CARTESIAN_POINT('Ctrl Pts',(-16.9592870711159,20.3674355779312,
21.6154977983717));
#204441=CARTESIAN_POINT('Ctrl Pts',(-17.0000461372983,20.4277127259959,
21.6111084608995));
#204442=CARTESIAN_POINT('Ctrl Pts',(-17.0438725612033,20.4858169439674,
21.6067191234274));
#204443=CARTESIAN_POINT('Ctrl Pts',(-17.0876339985392,20.5438350040133,
21.6023362945397));
#204444=CARTESIAN_POINT('Ctrl Pts',(-17.1344534764691,20.5996861485813,
21.597953465652));
#204445=CARTESIAN_POINT('Ctrl Pts',(-17.1840867418393,20.6530325558661,
21.5935706367643));
#204446=CARTESIAN_POINT('Ctrl Pts',(-17.2336617074652,20.7063163019118,
21.5891929559925));
#204447=CARTESIAN_POINT('Ctrl Pts',(-17.2860435680415,20.7571008040507,
21.5848152752207));
#204448=CARTESIAN_POINT('Ctrl Pts',(-17.3409474964239,20.8050808393179,
21.580437594449));
#204449=CARTESIAN_POINT('Ctrl Pts',(-17.3958166125325,20.853030452461,21.5760626893806));
#204450=CARTESIAN_POINT('Ctrl Pts',(-17.4532042613681,20.8981788105171,
21.5716877843123));
#204451=CARTESIAN_POINT('Ctrl Pts',(-17.512789428658,20.9402581474269,21.5673128792439));
#204452=CARTESIAN_POINT('Ctrl Pts',(-17.5723564435283,20.9823246650092,
21.5629393069756));
#204453=CARTESIAN_POINT('Ctrl Pts',(-17.6341192541722,21.0213237397462,
21.5585657347073));
#204454=CARTESIAN_POINT('Ctrl Pts',(-17.6977258376919,21.0570294852826,
21.5541921624389));
#204455=CARTESIAN_POINT('Ctrl Pts',(-17.7613339958298,21.0927361147356,
21.5498184819002));
#204456=CARTESIAN_POINT('Ctrl Pts',(-17.826785596102,21.1251490188774,21.5454448013616));
#204457=CARTESIAN_POINT('Ctrl Pts',(-17.8937033322731,21.1540878802069,
21.5410711208229));
#204458=CARTESIAN_POINT('Ctrl Pts',(-17.9606902956987,21.1830566791589,
21.5366929156557));
#204459=CARTESIAN_POINT('Ctrl Pts',(-18.0291459798704,21.2085440679544,
21.5323147104885));
#204460=CARTESIAN_POINT('Ctrl Pts',(-18.0986731480005,21.2304179337444,
21.5279365053214));
#204461=CARTESIAN_POINT('Ctrl Pts',(-18.1682381862999,21.2523037138266,
21.5235559154264));
#204462=CARTESIAN_POINT('Ctrl Pts',(-18.2388754035045,21.2705719312819,
21.5191753255314));
#204463=CARTESIAN_POINT('Ctrl Pts',(-18.3101750846391,21.2851411333656,
21.5147947356365));
#204464=CARTESIAN_POINT('Ctrl Pts',(-18.3816007583693,21.2997360804675,
21.5104064048669));
#204465=CARTESIAN_POINT('Ctrl Pts',(-18.4536907566283,21.3106188870059,
21.5060180740973));
#204466=CARTESIAN_POINT('Ctrl Pts',(-18.5260285057222,21.3177598006341,
21.5016297433277));
#204467=CARTESIAN_POINT('Ctrl Pts',(-18.5750325606489,21.3225972987322,
21.4986569386059));
#204468=CARTESIAN_POINT('Ctrl Pts',(-18.6241502208557,21.3257186676998,
21.4956841338842));
#204469=CARTESIAN_POINT('Ctrl Pts',(-18.6732524671973,21.3271282421579,
21.4927113291624));
#204470=CARTESIAN_POINT('Ctrl Pts',(-18.7457477304191,21.3292093581758,
21.4883222374839));
#204471=CARTESIAN_POINT('Ctrl Pts',(-18.8184908959863,21.3275648466035,
21.4839331458055));
#204472=CARTESIAN_POINT('Ctrl Pts',(-18.8910671061328,21.3221653000585,
21.479544054127));
#204473=CARTESIAN_POINT('Ctrl Pts',(-18.963535950148,21.316773741371,21.4751614554825));
#204474=CARTESIAN_POINT('Ctrl Pts',(-19.0358378521744,21.3076382108716,
21.4707788568379));
#204475=CARTESIAN_POINT('Ctrl Pts',(-19.1075565804157,21.2947812940009,
21.4663962581934));
#204476=CARTESIAN_POINT('Ctrl Pts',(-19.1791914639277,21.2819394078585,
21.462018783145));
#204477=CARTESIAN_POINT('Ctrl Pts',(-19.2502440557653,21.2653848625367,
21.4576413080965));
#204478=CARTESIAN_POINT('Ctrl Pts',(-19.3203035805939,21.2451920045519,
21.4532638330481));
#204479=CARTESIAN_POINT('Ctrl Pts',(-19.3903189251765,21.2250118803879,
21.4488891184798));
#204480=CARTESIAN_POINT('Ctrl Pts',(-19.4593419831433,21.2011981291416,
21.4445144039115));
#204481=CARTESIAN_POINT('Ctrl Pts',(-19.5269738982851,21.1738757975579,
21.4401396893431));
#204482=CARTESIAN_POINT('Ctrl Pts',(-19.5945854490439,21.1465616928952,
21.4357662920281));
#204483=CARTESIAN_POINT('Ctrl Pts',(-19.660806241817,21.1157412858172,21.4313928947131));
#204484=CARTESIAN_POINT('Ctrl Pts',(-19.7252558616825,21.0815883610993,
21.427019497398));
#204485=CARTESIAN_POINT('Ctrl Pts',(-19.7897073112052,21.0474344668156,
21.4226459759268));
#204486=CARTESIAN_POINT('Ctrl Pts',(-19.8523870628952,21.009948094583,21.4182724544556));
#204487=CARTESIAN_POINT('Ctrl Pts',(-19.9129393440597,20.9693489480272,
21.4138989329844));
#204488=CARTESIAN_POINT('Ctrl Pts',(-19.9735546264146,20.9287075603778,
21.4095208611139));
#204489=CARTESIAN_POINT('Ctrl Pts',(-20.0320376175176,20.884947201305,21.4051427892433));
#204490=CARTESIAN_POINT('Ctrl Pts',(-20.0880622982485,20.8383304189568,
21.4007647173728));
#204491=CARTESIAN_POINT('Ctrl Pts',(-20.1441176775265,20.7916880930897,
21.3963842465516));
#204492=CARTESIAN_POINT('Ctrl Pts',(-20.1977117100799,20.742186555063,21.3920037757304));
#204493=CARTESIAN_POINT('Ctrl Pts',(-20.2485542308315,20.6901262562305,
21.3876233049092));
#204494=CARTESIAN_POINT('Ctrl Pts',(-20.2994868807634,20.6379736694469,
21.3832350687719));
#204495=CARTESIAN_POINT('Ctrl Pts',(-20.3476579595779,20.583253625968,21.3788468326346));
#204496=CARTESIAN_POINT('Ctrl Pts',(-20.3928170701038,20.5263003185327,
21.3744585964973));
#204497=CARTESIAN_POINT('Ctrl Pts',(-20.4234260340952,20.4876972168291,
21.3714842384918));
#204498=CARTESIAN_POINT('Ctrl Pts',(-20.4526521165783,20.4480687834689,
21.3685098804864));
#204499=CARTESIAN_POINT('Ctrl Pts',(-20.4804290561878,20.407526034695,21.3655355224809));
#204500=CARTESIAN_POINT('Ctrl Pts',(-20.5219934576021,20.3468593410935,
21.3610848014214));
#204501=CARTESIAN_POINT('Ctrl Pts',(-20.5604706135638,20.283911430233,21.3566340803619));
#204502=CARTESIAN_POINT('Ctrl Pts',(-20.5956058292723,20.2190241745213,
21.3521833593024));
#204503=CARTESIAN_POINT('Ctrl Pts',(-20.6306759483131,20.154257138482,21.3477408843033));
#204504=CARTESIAN_POINT('Ctrl Pts',(-20.6624162151988,20.0875583047225,
21.3432984093041));
#204505=CARTESIAN_POINT('Ctrl Pts',(-20.6906150299305,20.0192985986937,
21.338855934305));
#204506=CARTESIAN_POINT('Ctrl Pts',(-20.7018340902154,19.9921410828813,
21.3370884701295));
#204507=CARTESIAN_POINT('Ctrl Pts',(-20.7124930633451,19.9647368113629,
21.335321005954));
#204508=CARTESIAN_POINT('Ctrl Pts',(-20.7225806064498,19.9371103026755,
21.3335535417785));
#204509=CARTESIAN_POINT('',(-17.1140743056112,17.8480877707428,22.));
#204510=CARTESIAN_POINT('Origin',(-18.734,19.211,22.));
#204511=CARTESIAN_POINT('Ctrl Pts',(-20.7225806064499,19.9371103026755,
21.5555703710623));
#204512=CARTESIAN_POINT('Ctrl Pts',(-20.6978891140345,20.0047322917599,
21.5598847349407));
#204513=CARTESIAN_POINT('Ctrl Pts',(-20.669739933046,20.071105290786,21.564199098819));
#204514=CARTESIAN_POINT('Ctrl Pts',(-20.6382937973645,20.1358535739883,
21.5685134626974));
#204515=CARTESIAN_POINT('Ctrl Pts',(-20.6068209721235,20.2006568115793,
21.5728314883444));
#204516=CARTESIAN_POINT('Ctrl Pts',(-20.5720458189299,20.263832130486,21.5771495139913));
#204517=CARTESIAN_POINT('Ctrl Pts',(-20.5341758702126,20.3250268561863,
21.5814675396383));
#204518=CARTESIAN_POINT('Ctrl Pts',(-20.496290452322,20.3862465787997,21.5857873291188));
#204519=CARTESIAN_POINT('Ctrl Pts',(-20.4553080047756,20.4454836883216,
21.5901071185994));
#204520=CARTESIAN_POINT('Ctrl Pts',(-20.4114788047957,20.5024154480496,
21.5944269080799));
#204521=CARTESIAN_POINT('Ctrl Pts',(-20.3675728312531,20.5594469324823,
21.5987542643339));
#204522=CARTESIAN_POINT('Ctrl Pts',(-20.3208104691955,20.61416462363,21.603081620588));
#204523=CARTESIAN_POINT('Ctrl Pts',(-20.271481140103,20.6662802973406,21.607408976842));
#204524=CARTESIAN_POINT('Ctrl Pts',(-20.2294416062698,20.7106944150369,
21.6110968445466));
#204525=CARTESIAN_POINT('Ctrl Pts',(-20.1855384995037,20.7532192421642,
21.6147847122511));
#204526=CARTESIAN_POINT('Ctrl Pts',(-20.1399695343548,20.7936998036476,
21.6184725799557));
#204527=CARTESIAN_POINT('Ctrl Pts',(-20.0856806209084,20.8419266108937,
21.6228661475946));
#204528=CARTESIAN_POINT('Ctrl Pts',(-20.0288044225739,20.8874484514206,
21.6272597152335));
#204529=CARTESIAN_POINT('Ctrl Pts',(-19.969641252187,20.9299763511735,21.6316532828724));
#204530=CARTESIAN_POINT('Ctrl Pts',(-19.9105643807625,20.9724422171712,
21.636040441789));
#204531=CARTESIAN_POINT('Ctrl Pts',(-19.8492075475796,21.0119225341567,
21.6404276007057));
#204532=CARTESIAN_POINT('Ctrl Pts',(-19.7859054205824,21.0481673810922,
21.6448147596223));
#204533=CARTESIAN_POINT('Ctrl Pts',(-19.7226757606736,21.0843707356065,
21.6491968962016));
#204534=CARTESIAN_POINT('Ctrl Pts',(-19.6575056463759,21.1173457404981,
21.6535790327809));
#204535=CARTESIAN_POINT('Ctrl Pts',(-19.5907587261482,21.1468857107714,
21.6579611693602));
#204536=CARTESIAN_POINT('Ctrl Pts',(-19.5240529471155,21.176407473318,21.6623406048961));
#204537=CARTESIAN_POINT('Ctrl Pts',(-19.455772729471,21.2024982084514,21.6667200404319));
#204538=CARTESIAN_POINT('Ctrl Pts',(-19.386305067273,21.2249977902694,21.6710994759677));
#204539=CARTESIAN_POINT('Ctrl Pts',(-19.3168574801294,21.2474908700645,
21.675477645916));
#204540=CARTESIAN_POINT('Ctrl Pts',(-19.2462235870209,21.2663947090104,
21.6798558158643));
#204541=CARTESIAN_POINT('Ctrl Pts',(-19.1748074790921,21.2815984077982,
21.6842339858126));
#204542=CARTESIAN_POINT('Ctrl Pts',(-19.1033886290298,21.2968026903559,
21.6886123238676));
#204543=CARTESIAN_POINT('Ctrl Pts',(-19.0311879752794,21.3083064524741,
21.6929906619226));
#204544=CARTESIAN_POINT('Ctrl Pts',(-18.9586201563124,21.3160498296663,
21.6973689999776));
#204545=CARTESIAN_POINT('Ctrl Pts',(-18.8859763854438,21.3238013113356,
21.7017519205474));
#204546=CARTESIAN_POINT('Ctrl Pts',(-18.8129651613083,21.3277844990936,
21.7061348411171));
#204547=CARTESIAN_POINT('Ctrl Pts',(-18.7400057927391,21.3279914809591,
21.7105177616869));
#204548=CARTESIAN_POINT('Ctrl Pts',(-18.6670060696851,21.3281985773082,
21.7149031064896));
#204549=CARTESIAN_POINT('Ctrl Pts',(-18.5940587399491,21.324625332556,21.7192884512922));
#204550=CARTESIAN_POINT('Ctrl Pts',(-18.5215799495223,21.3173159122399,
21.7236737960949));
#204551=CARTESIAN_POINT('Ctrl Pts',(-18.4489730689547,21.3099935741492,
21.7280668910191));
#204552=CARTESIAN_POINT('Ctrl Pts',(-18.3768368570159,21.2989219477123,
21.7324599859432));
#204553=CARTESIAN_POINT('Ctrl Pts',(-18.3055786328723,21.284196597573,21.7368530808674));
#204554=CARTESIAN_POINT('Ctrl Pts',(-18.2580238618236,21.2743695121678,
21.7397848494573));
#204555=CARTESIAN_POINT('Ctrl Pts',(-18.2108598781007,21.2629162374029,
21.7427166180472));
#204556=CARTESIAN_POINT('Ctrl Pts',(-18.1642034712006,21.2498773665349,
21.7456483866371));
#204557=CARTESIAN_POINT('Ctrl Pts',(-18.0951059728948,21.230566977725,21.7499902956831));
#204558=CARTESIAN_POINT('Ctrl Pts',(-18.0268401014068,21.2076976293853,
21.754332204729));
#204559=CARTESIAN_POINT('Ctrl Pts',(-17.959804544219,21.1813579360736,21.758674113775));
#204560=CARTESIAN_POINT('Ctrl Pts',(-17.8928699309423,21.1550579057671,
21.7630094846598));
#204561=CARTESIAN_POINT('Ctrl Pts',(-17.8271624114981,21.1252980759476,
21.7673448555445));
#204562=CARTESIAN_POINT('Ctrl Pts',(-17.7630671934661,21.0922172881398,
21.7716802264293));
#204563=CARTESIAN_POINT('Ctrl Pts',(-17.6990456418676,21.0591745210102,
21.7760106145506));
#204564=CARTESIAN_POINT('Ctrl Pts',(-17.6366331495171,21.0228185970339,
21.7803410026719));
#204565=CARTESIAN_POINT('Ctrl Pts',(-17.5761948535926,20.9833363797407,
21.7846713907932));
#204566=CARTESIAN_POINT('Ctrl Pts',(-17.5157937013986,20.9438784271429,
21.7889991175759));
#204567=CARTESIAN_POINT('Ctrl Pts',(-17.4573647522916,20.9012982594394,
21.7933268443586));
#204568=CARTESIAN_POINT('Ctrl Pts',(-17.4012470250051,20.8558278048605,
21.7976545711413));
#204569=CARTESIAN_POINT('Ctrl Pts',(-17.3451443445715,20.81036954228,21.8019811375301));
#204570=CARTESIAN_POINT('Ctrl Pts',(-17.2913520397843,20.7620228406339,
21.8063077039189));
#204571=CARTESIAN_POINT('Ctrl Pts',(-17.2401772158046,20.7110608285729,
21.8106342703077));
#204572=CARTESIAN_POINT('Ctrl Pts',(-17.1889983840908,20.6600948254439,
21.8149611755297));
#204573=CARTESIAN_POINT('Ctrl Pts',(-17.1404377881069,20.6065134551268,
21.8192880807517));
#204574=CARTESIAN_POINT('Ctrl Pts',(-17.0947654083712,20.5506264231522,
21.8236149859736));
#204575=CARTESIAN_POINT('Ctrl Pts',(-17.0490382189606,20.4946723232895,
21.827947083749));
#204576=CARTESIAN_POINT('Ctrl Pts',(-17.0062064773784,20.4364074215726,
21.8322791815243));
#204577=CARTESIAN_POINT('Ctrl Pts',(-16.9664990268283,20.3761735106142,
21.8366112792996));
#204578=CARTESIAN_POINT('Ctrl Pts',(-16.9267670699395,20.3159024249543,
21.8409460507257));
#204579=CARTESIAN_POINT('Ctrl Pts',(-16.8901634882159,20.2536603390498,
21.8452808221518));
#204580=CARTESIAN_POINT('Ctrl Pts',(-16.856871493227,20.1898143690508,21.8496155935779));
#204581=CARTESIAN_POINT('Ctrl Pts',(-16.8235124512874,20.1258398192654,
21.8539590948264));
#204582=CARTESIAN_POINT('Ctrl Pts',(-16.7934785159735,20.060255385527,21.858302596075));
#204583=CARTESIAN_POINT('Ctrl Pts',(-16.7669047947946,19.9934483712413,
21.8626460973235));
#204584=CARTESIAN_POINT('Ctrl Pts',(-16.7461481233425,19.9412655686561,
21.8660387959885));
#204585=CARTESIAN_POINT('Ctrl Pts',(-16.7275016016086,19.8883372861217,
21.8694314946536));
#204586=CARTESIAN_POINT('Ctrl Pts',(-16.7110080073322,19.8348528653473,
21.8728241933186));
#204587=CARTESIAN_POINT('Ctrl Pts',(-16.6890808041098,19.7637486691424,
21.8773345742491));
#204588=CARTESIAN_POINT('Ctrl Pts',(-16.6708715122103,19.691373744136,21.8818449551797));
#204589=CARTESIAN_POINT('Ctrl Pts',(-16.6565194069635,19.6181404985465,
21.8863553361102));
#204590=CARTESIAN_POINT('Ctrl Pts',(-16.6414519418388,19.5412570480063,
21.891090530439));
#204591=CARTESIAN_POINT('Ctrl Pts',(-16.6306364194547,19.4634279279486,
21.8958257247677));
#204592=CARTESIAN_POINT('Ctrl Pts',(-16.6241751632239,19.3851498151671,
21.9005609190965));
#204593=CARTESIAN_POINT('Ctrl Pts',(-16.618041130639,19.3108360165285,21.9050563044009));
#204594=CARTESIAN_POINT('Ctrl Pts',(-16.6158311432077,19.2361181121913,
21.9095516897054));
#204595=CARTESIAN_POINT('Ctrl Pts',(-16.6175804022592,19.1614309945752,
21.9140470750099));
#204596=CARTESIAN_POINT('Ctrl Pts',(-16.6193280165078,19.0868141041766,
21.9185382333685));
#204597=CARTESIAN_POINT('Ctrl Pts',(-16.6250274669155,19.0122283910569,
21.9230293917272));
#204598=CARTESIAN_POINT('Ctrl Pts',(-16.6346619440205,18.9381104129575,
21.9275205500858));
#204599=CARTESIAN_POINT('Ctrl Pts',(-16.644289879149,18.8640427622465,21.9320086588702));
#204600=CARTESIAN_POINT('Ctrl Pts',(-16.6578474702978,18.7904426603016,
21.9364967676547));
#204601=CARTESIAN_POINT('Ctrl Pts',(-16.6752660492705,18.7177419335545,
21.9409848764392));
#204602=CARTESIAN_POINT('Ctrl Pts',(-16.6926773473537,18.6450715953915,
21.9454711092139));
#204603=CARTESIAN_POINT('Ctrl Pts',(-16.7139463177063,18.5733003216091,
21.9499573419886));
#204604=CARTESIAN_POINT('Ctrl Pts',(-16.7389533863518,18.5028488795668,
21.9544435747634));
#204605=CARTESIAN_POINT('Ctrl Pts',(-16.7639635634828,18.432388680109,21.958930365196));
#204606=CARTESIAN_POINT('Ctrl Pts',(-16.7927126236932,18.363249066819,21.9634171556287));
#204607=CARTESIAN_POINT('Ctrl Pts',(-16.8250316763889,18.2958339279402,
21.9679039460613));
#204608=CARTESIAN_POINT('Ctrl Pts',(-16.8573522841798,18.2284155452484,
21.9723909523848));
#204609=CARTESIAN_POINT('Ctrl Pts',(-16.8932430249613,18.1627222047342,
21.9768779587083));
#204610=CARTESIAN_POINT('Ctrl Pts',(-16.9324883220855,18.0991345970228,
21.9813649650317));
#204611=CARTESIAN_POINT('Ctrl Pts',(-16.9717607058636,18.0355031018739,
21.9858550682355));
#204612=CARTESIAN_POINT('Ctrl Pts',(-17.0143920255779,17.9739806203857,
21.9903451714393));
#204613=CARTESIAN_POINT('Ctrl Pts',(-17.0601229488358,17.9149195173194,
21.994835274643));
#204614=CARTESIAN_POINT('Ctrl Pts',(-17.0776568931743,17.8922745755608,
21.996556849762));
#204615=CARTESIAN_POINT('Ctrl Pts',(-17.0956460703827,17.8699911414134,
21.998278424881));
#204616=CARTESIAN_POINT('Ctrl Pts',(-17.1140743056111,17.8480877707428,
22.));
#204617=CARTESIAN_POINT('Origin',(18.734,19.211,0.));
#204618=CARTESIAN_POINT('',(17.1140599594606,17.8481048224249,21.9999997809097));
#204619=CARTESIAN_POINT('Ctrl Pts',(17.1140599594606,17.8481048224249,21.9999997809097));
#204620=CARTESIAN_POINT('Ctrl Pts',(17.1607068911252,17.7926601825033,21.9956147575322));
#204621=CARTESIAN_POINT('Ctrl Pts',(17.2102952620655,17.739504224746,21.9912297341546));
#204622=CARTESIAN_POINT('Ctrl Pts',(17.2625716911555,17.6889659228745,21.9868447107771));
#204623=CARTESIAN_POINT('Ctrl Pts',(17.3147705007786,17.6385026597179,21.9824661982341));
#204624=CARTESIAN_POINT('Ctrl Pts',(17.3696491012488,17.5906496701831,21.9780876856911));
#204625=CARTESIAN_POINT('Ctrl Pts',(17.4269143514077,17.5457023967939,21.9737091731481));
#204626=CARTESIAN_POINT('Ctrl Pts',(17.4841122081179,17.5008080202619,21.9693358135217));
#204627=CARTESIAN_POINT('Ctrl Pts',(17.5436907567674,17.4588128636585,21.9649624538953));
#204628=CARTESIAN_POINT('Ctrl Pts',(17.605321823504,17.4199738768232,21.960589094269));
#204629=CARTESIAN_POINT('Ctrl Pts',(17.6669138937314,17.3811594650113,21.956218501847));
#204630=CARTESIAN_POINT('Ctrl Pts',(17.7305554975065,17.3454975176011,21.951847909425));
#204631=CARTESIAN_POINT('Ctrl Pts',(17.7958885256649,17.3132023654455,21.947477317003));
#204632=CARTESIAN_POINT('Ctrl Pts',(17.8612018513836,17.2809169525184,21.9431080426178));
#204633=CARTESIAN_POINT('Ctrl Pts',(17.9282051559123,17.2519965330214,21.9387387682326));
#204634=CARTESIAN_POINT('Ctrl Pts',(17.9965162100301,17.2266092472671,21.9343694938474));
#204635=CARTESIAN_POINT('Ctrl Pts',(18.0648292857548,17.2012212101981,21.9300000901573));
#204636=CARTESIAN_POINT('Ctrl Pts',(18.1344497342609,17.179366680706,21.9256306864672));
#204637=CARTESIAN_POINT('Ctrl Pts',(18.2049774492685,17.1611648503313,21.9212612827771));
#204638=CARTESIAN_POINT('Ctrl Pts',(18.275576959088,17.142944491113,21.9168874311828));
#204639=CARTESIAN_POINT('Ctrl Pts',(18.3470851103194,17.1283843746466,21.9125135795885));
#204640=CARTESIAN_POINT('Ctrl Pts',(18.4190896618186,17.1175529672556,21.9081397279943));
#204641=CARTESIAN_POINT('Ctrl Pts',(18.4911340360637,17.1067155694601,21.9037634574032));
#204642=CARTESIAN_POINT('Ctrl Pts',(18.5636748760598,17.0996110331389,21.8993871868121));
#204643=CARTESIAN_POINT('Ctrl Pts',(18.6362955339105,17.0962558458986,21.895010916221));
#204644=CARTESIAN_POINT('Ctrl Pts',(18.7090403295018,17.0928949233017,21.8906271648337));
#204645=CARTESIAN_POINT('Ctrl Pts',(18.7818647321215,17.0932961427629,21.8862434134464));
#204646=CARTESIAN_POINT('Ctrl Pts',(18.8543534992707,17.0974238752263,21.8818596620591));
#204647=CARTESIAN_POINT('Ctrl Pts',(18.8963594228442,17.0998158211955,21.879319357775));
#204648=CARTESIAN_POINT('Ctrl Pts',(18.9382527448405,17.103458157136,21.8767790534908));
#204649=CARTESIAN_POINT('Ctrl Pts',(18.9799541720406,17.1083360836178,21.8742387492067));
#204650=CARTESIAN_POINT('Ctrl Pts',(19.0521148556278,17.1167769100605,21.8698429741465));
#204651=CARTESIAN_POINT('Ctrl Pts',(19.1239758590327,17.1289525413789,21.8654471990862));
#204652=CARTESIAN_POINT('Ctrl Pts',(19.1951213352851,17.1448305698358,21.861051424026));
#204653=CARTESIAN_POINT('Ctrl Pts',(19.2661639857042,17.1606856499397,21.8566620021347));
#204654=CARTESIAN_POINT('Ctrl Pts',(19.3364926969102,17.1802323993941,21.8522725802435));
#204655=CARTESIAN_POINT('Ctrl Pts',(19.4056979848776,17.2033867859791,21.8478831583522));
#204656=CARTESIAN_POINT('Ctrl Pts',(19.4748252563206,17.2265150701546,21.8434986847453));
#204657=CARTESIAN_POINT('Ctrl Pts',(19.5428311670215,17.2532427601722,21.8391142111383));
#204658=CARTESIAN_POINT('Ctrl Pts',(19.6093192809603,17.2834354339272,21.8347297375313));
#204659=CARTESIAN_POINT('Ctrl Pts',(19.6757671116488,17.3136098148032,21.8303479203518));
#204660=CARTESIAN_POINT('Ctrl Pts',(19.7406985339571,17.3472448153046,21.8259661031722));
#204661=CARTESIAN_POINT('Ctrl Pts',(19.8037363887647,17.3841576262434,21.8215842859927));
#204662=CARTESIAN_POINT('Ctrl Pts',(19.8667566375372,17.4210601276904,21.8172036926242));
#204663=CARTESIAN_POINT('Ctrl Pts',(19.9278839545639,17.4612383791652,21.8128230992558));
#204664=CARTESIAN_POINT('Ctrl Pts',(19.9867665975567,17.5044640783018,21.8084425058873));
#204665=CARTESIAN_POINT('Ctrl Pts',(20.0456520241437,17.5476918208727,21.8040617054325));
#204666=CARTESIAN_POINT('Ctrl Pts',(20.1022921799,17.5939670112651,21.7996809049776));
#204667=CARTESIAN_POINT('Ctrl Pts',(20.156366438267,17.6430195424395,21.7953001045228));
#204668=CARTESIAN_POINT('Ctrl Pts',(20.2104978161903,17.6921238886346,21.7909146765541));
#204669=CARTESIAN_POINT('Ctrl Pts',(20.2620575288253,17.7440111093862,21.7865292485854));
#204670=CARTESIAN_POINT('Ctrl Pts',(20.3107606507593,17.7983730675734,21.7821438206167));
#204671=CARTESIAN_POINT('Ctrl Pts',(20.3594910179605,17.8527654366668,21.777755939373));
#204672=CARTESIAN_POINT('Ctrl Pts',(20.4053613108282,17.9096349255095,21.7733680581292));
#204673=CARTESIAN_POINT('Ctrl Pts',(20.4481276048669,17.9686411330726,21.7689801768854));
#204674=CARTESIAN_POINT('Ctrl Pts',(20.4909696354496,18.0277518370932,21.7645845249669));
#204675=CARTESIAN_POINT('Ctrl Pts',(20.5306964282269,18.0890064129735,21.7601888730484));
#204676=CARTESIAN_POINT('Ctrl Pts',(20.56710831572,18.1520368737118,21.7557932211298));
#204677=CARTESIAN_POINT('Ctrl Pts',(20.5912144042082,18.1937654950115,21.7528831282617));
#204678=CARTESIAN_POINT('Ctrl Pts',(20.6138685324289,18.2362719576463,21.7499730353935));
#204679=CARTESIAN_POINT('Ctrl Pts',(20.6350243872034,18.2794446987657,21.7470629425253));
#204680=CARTESIAN_POINT('Ctrl Pts',(20.6668849874923,18.3444626081263,21.7426803587599));
#204681=CARTESIAN_POINT('Ctrl Pts',(20.6954698849173,18.4112469909798,21.7382977749946));
#204682=CARTESIAN_POINT('Ctrl Pts',(20.720580017359,18.4794339847767,21.7339151912293));
#204683=CARTESIAN_POINT('Ctrl Pts',(20.7456523700338,18.5475183869707,21.7295392013357));
#204684=CARTESIAN_POINT('Ctrl Pts',(20.7672601692967,18.6170007611369,21.7251632114421));
#204685=CARTESIAN_POINT('Ctrl Pts',(20.7852510315621,18.6874943118595,21.7207872215485));
#204686=CARTESIAN_POINT('Ctrl Pts',(20.8032203398046,18.7579034075081,21.7164164743267));
#204687=CARTESIAN_POINT('Ctrl Pts',(20.8175811995767,18.8293208069692,21.7120457271049));
#204688=CARTESIAN_POINT('Ctrl Pts',(20.8282305540802,18.9013431151147,21.7076749798831));
#204689=CARTESIAN_POINT('Ctrl Pts',(20.838873012161,18.9733187822846,21.7033070631165));
#204690=CARTESIAN_POINT('Ctrl Pts',(20.8458086628383,19.0458981036007,21.6989391463499));
#204691=CARTESIAN_POINT('Ctrl Pts',(20.848985506631,19.1186674123577,21.6945712295833));
#204692=CARTESIAN_POINT('Ctrl Pts',(20.8521613485358,19.1914137717031,21.6902046903359));
#204693=CARTESIAN_POINT('Ctrl Pts',(20.8515807156441,19.2643495165153,21.6858381510884));
#204694=CARTESIAN_POINT('Ctrl Pts',(20.8472435998573,19.3370574776133,21.681471611841));
#204695=CARTESIAN_POINT('Ctrl Pts',(20.8429064110345,19.4097666630956,21.6771049990621));
#204696=CARTESIAN_POINT('Ctrl Pts',(20.8348126445421,19.4822475744202,21.6727383862833));
#204697=CARTESIAN_POINT('Ctrl Pts',(20.8230142986461,19.5540863740405,21.6683717735044));
#204698=CARTESIAN_POINT('Ctrl Pts',(20.8112037407264,19.6259995312979,21.664000641009));
#204699=CARTESIAN_POINT('Ctrl Pts',(20.7956810261304,19.6972687714271,21.6596295085136));
#204700=CARTESIAN_POINT('Ctrl Pts',(20.7765494845939,19.7674895353779,21.6552583760183));
#204701=CARTESIAN_POINT('Ctrl Pts',(20.7574075663198,19.8377483862984,21.6508848726687));
#204702=CARTESIAN_POINT('Ctrl Pts',(20.7346530755002,19.906957168973,21.6465113693192));
#204703=CARTESIAN_POINT('Ctrl Pts',(20.7084387039386,19.9747282267858,21.6421378659696));
#204704=CARTESIAN_POINT('Ctrl Pts',(20.6821775964101,20.0426201093875,21.637756565374));
#204705=CARTESIAN_POINT('Ctrl Pts',(20.6524444880472,20.109068706537,21.6333752647783));
#204706=CARTESIAN_POINT('Ctrl Pts',(20.6194392664437,20.1737085605479,21.6289939641826));
#204707=CARTESIAN_POINT('Ctrl Pts',(20.5965714078508,20.2184946570858,21.6259583547363));
#204708=CARTESIAN_POINT('Ctrl Pts',(20.572133749745,20.2624129761557,21.6229227452901));
#204709=CARTESIAN_POINT('Ctrl Pts',(20.5462048156797,20.3053503579875,21.6198871358438));
#204710=CARTESIAN_POINT('Ctrl Pts',(20.5087128685692,20.3674356733592,21.6154977957915));
#204711=CARTESIAN_POINT('Ctrl Pts',(20.4679537734929,20.4277128557231,21.6111084557392));
#204712=CARTESIAN_POINT('Ctrl Pts',(20.4241273179606,20.4858171041695,21.6067191156869));
#204713=CARTESIAN_POINT('Ctrl Pts',(20.3803658487493,20.5438351950362,21.6023362841933));
#204714=CARTESIAN_POINT('Ctrl Pts',(20.3335463361778,20.5996863665837,21.5979534526998));
#204715=CARTESIAN_POINT('Ctrl Pts',(20.2839130339366,20.6530327968647,21.5935706212063));
#204716=CARTESIAN_POINT('Ctrl Pts',(20.2343380311571,20.70631656623,21.5891929378029));
#204717=CARTESIAN_POINT('Ctrl Pts',(20.1819561311663,20.7571010876826,21.5848152543996));
#204718=CARTESIAN_POINT('Ctrl Pts',(20.1270521616165,20.8050811381531,21.5804375709962));
#204719=CARTESIAN_POINT('Ctrl Pts',(20.0721830041647,20.8530307666663,21.5760626632818));
#204720=CARTESIAN_POINT('Ctrl Pts',(20.0147953122166,20.8981791359674,21.5716877555675));
#204721=CARTESIAN_POINT('Ctrl Pts',(19.9552101005245,20.9402584799205,21.5673128478531));
#204722=CARTESIAN_POINT('Ctrl Pts',(19.8956430411106,20.9823250046532,21.5629392729282));
#204723=CARTESIAN_POINT('Ctrl Pts',(19.8338801846224,21.0213240823263,21.5585656980033));
#204724=CARTESIAN_POINT('Ctrl Pts',(19.7702735544122,21.0570298265266,21.5541921230784));
#204725=CARTESIAN_POINT('Ctrl Pts',(19.7066653494861,21.0927364546977,21.5498184398764));
#204726=CARTESIAN_POINT('Ctrl Pts',(19.6412137015734,21.1251493532758,21.5454447566744));
#204727=CARTESIAN_POINT('Ctrl Pts',(19.574295917344,21.154088204713,21.5410710734725));
#204728=CARTESIAN_POINT('Ctrl Pts',(19.5073089059773,21.1830569936903,21.5366928656502));
#204729=CARTESIAN_POINT('Ctrl Pts',(19.4388531734526,21.2085443681914,21.5323146578279));
#204730=CARTESIAN_POINT('Ctrl Pts',(19.3693259569769,21.2304182153262,21.5279364500056));
#204731=CARTESIAN_POINT('Ctrl Pts',(19.2997608703362,21.2523039767335,21.523555857456));
#204732=CARTESIAN_POINT('Ctrl Pts',(19.2291236047978,21.270572171152,21.5191752649063));
#204733=CARTESIAN_POINT('Ctrl Pts',(19.1578238757517,21.2851413457966,21.5147946723567));
#204734=CARTESIAN_POINT('Ctrl Pts',(19.086398154594,21.2997362652946,21.5104063389627));
#204735=CARTESIAN_POINT('Ctrl Pts',(19.0143081093411,21.3106190398704,21.5060180055687));
#204736=CARTESIAN_POINT('Ctrl Pts',(18.9419703140981,21.3177599171367,21.5016296721748));
#204737=CARTESIAN_POINT('Ctrl Pts',(18.8929666481794,21.3225973491147,21.4986568911707));
#204738=CARTESIAN_POINT('Ctrl Pts',(18.8438493793155,21.3257186793944,21.4956841101665));
#204739=CARTESIAN_POINT('Ctrl Pts',(18.7947475234683,21.3271282424259,21.4927113291624));
#204740=CARTESIAN_POINT('Ctrl Pts',(18.7222522479351,21.3292093584771,21.4883222368506));
#204741=CARTESIAN_POINT('Ctrl Pts',(18.6495090705527,21.3275648456576,21.4839331445389));
#204742=CARTESIAN_POINT('Ctrl Pts',(18.576932849213,21.3221652967363,21.4795440522271));
#204743=CARTESIAN_POINT('Ctrl Pts',(18.5044639937146,21.3167737356532,21.4751614529316));
#204744=CARTESIAN_POINT('Ctrl Pts',(18.4321620808264,21.3076382016009,21.4707788536361));
#204745=CARTESIAN_POINT('Ctrl Pts',(18.3604433424476,21.2947812801727,21.4663962543406));
#204746=CARTESIAN_POINT('Ctrl Pts',(18.2888084484159,21.2819393894075,21.4620187786179));
#204747=CARTESIAN_POINT('Ctrl Pts',(18.2177558467876,21.2653848384199,21.4576413028952));
#204748=CARTESIAN_POINT('Ctrl Pts',(18.1476963129808,21.2451919738775,21.4532638271725));
#204749=CARTESIAN_POINT('Ctrl Pts',(18.0776809591945,21.2250118430934,21.4488891119159));
#204750=CARTESIAN_POINT('Ctrl Pts',(18.0086578928418,21.2011980843124,21.4445143966593));
#204751=CARTESIAN_POINT('Ctrl Pts',(17.9410259701971,21.1738757444266,21.4401396814027));
#204752=CARTESIAN_POINT('Ctrl Pts',(17.8734144117325,21.1465616313814,21.4357662833863));
#204753=CARTESIAN_POINT('Ctrl Pts',(17.8071936121441,21.1157412151327,21.43139288537));
#204754=CARTESIAN_POINT('Ctrl Pts',(17.7427439864028,21.0815882805972,21.4270194873536));
#204755=CARTESIAN_POINT('Ctrl Pts',(17.6782925308258,21.0474343764011,21.4226459651689));
#204756=CARTESIAN_POINT('Ctrl Pts',(17.6156127740304,21.0099479935908,21.4182724429842));
#204757=CARTESIAN_POINT('Ctrl Pts',(17.5550604887456,20.9693488359262,21.4138989207996));
#204758=CARTESIAN_POINT('Ctrl Pts',(17.4944452020835,20.9287074370344,21.4095208482016));
#204759=CARTESIAN_POINT('Ctrl Pts',(17.4359622076729,20.8849470661681,21.4051427756037));
#204760=CARTESIAN_POINT('Ctrl Pts',(17.3799375246599,20.8383302716031,21.4007647030058));
#204761=CARTESIAN_POINT('Ctrl Pts',(17.3238821429895,20.7916879334218,21.3963842314483));
#204762=CARTESIAN_POINT('Ctrl Pts',(17.2702881090797,20.742186382646,21.3920037598908));
#204763=CARTESIAN_POINT('Ctrl Pts',(17.2194455880258,20.690126070749,21.3876232883333));
#204764=CARTESIAN_POINT('Ctrl Pts',(17.1685129377324,20.6379734708179,21.3832350514533));
#204765=CARTESIAN_POINT('Ctrl Pts',(17.1203418596204,20.5832534138692,21.3788468145733));
#204766=CARTESIAN_POINT('Ctrl Pts',(17.0751827508733,20.5263000927544,21.3744585776934));
#204767=CARTESIAN_POINT('Ctrl Pts',(17.0445738577713,20.4876970696618,21.3714842259559));
#204768=CARTESIAN_POINT('Ctrl Pts',(17.0153478403718,20.4480687194866,21.3685098742184));
#204769=CARTESIAN_POINT('Ctrl Pts',(16.9875709596013,20.4075260577406,21.3655355224809));
#204770=CARTESIAN_POINT('Ctrl Pts',(16.9460065700333,20.3468593831467,21.3610848026413));
#204771=CARTESIAN_POINT('Ctrl Pts',(16.9075294235406,20.2839114919535,21.3566340828016));
#204772=CARTESIAN_POINT('Ctrl Pts',(16.8723942149818,20.2190242562492,21.3521833629619));
#204773=CARTESIAN_POINT('Ctrl Pts',(16.837324103298,20.1542572405875,21.3477408892083));
#204774=CARTESIAN_POINT('Ctrl Pts',(16.8055838414173,20.0875584275687,21.3432984154547));
#204775=CARTESIAN_POINT('Ctrl Pts',(16.7773850294157,20.0192987423505,21.3388559417011));
#204776=CARTESIAN_POINT('Ctrl Pts',(16.7661659358305,19.9921411515798,21.3370884726039));
#204777=CARTESIAN_POINT('Ctrl Pts',(16.7555069324745,19.9647368036015,21.3353210035066));
#204778=CARTESIAN_POINT('Ctrl Pts',(16.7454193623258,19.9371102171621,21.3335535344094));
#204779=CARTESIAN_POINT('',(20.3539256943888,17.8480877707428,22.));
#204780=CARTESIAN_POINT('Origin',(18.734,19.211,22.));
#204781=CARTESIAN_POINT('Ctrl Pts',(16.7454193623258,19.9371102171621,21.5555703650724));
#204782=CARTESIAN_POINT('Ctrl Pts',(16.7701108524687,20.0047322090483,21.5598847289556));
#204783=CARTESIAN_POINT('Ctrl Pts',(16.7982600312914,20.0711052106196,21.5641990928389));
#204784=CARTESIAN_POINT('Ctrl Pts',(16.8297061648234,20.1358534961323,21.5685134567221));
#204785=CARTESIAN_POINT('Ctrl Pts',(16.8611789881103,20.2006567364418,21.572831482401));
#204786=CARTESIAN_POINT('Ctrl Pts',(16.8959541394072,20.2638320578116,21.5771495080799));
#204787=CARTESIAN_POINT('Ctrl Pts',(16.9338240862002,20.3250267857529,21.5814675337588));
#204788=CARTESIAN_POINT('Ctrl Pts',(16.9717095022942,20.3862465108161,21.585787323286));
#204789=CARTESIAN_POINT('Ctrl Pts',(17.0126919480371,20.4454836225521,21.5901071128131));
#204790=CARTESIAN_POINT('Ctrl Pts',(17.0565211461299,20.5024153843046,21.5944269023403));
#204791=CARTESIAN_POINT('Ctrl Pts',(17.100427118034,20.5594468710926,21.5987542586658));
#204792=CARTESIAN_POINT('Ctrl Pts',(17.1471894784021,20.6141645643789,21.6030816149914));
#204793=CARTESIAN_POINT('Ctrl Pts',(17.1965188056852,20.6662802400666,21.6074089713169));
#204794=CARTESIAN_POINT('Ctrl Pts',(17.2385583582755,20.7106943808936,21.6110968408632));
#204795=CARTESIAN_POINT('Ctrl Pts',(17.2824614855129,20.7532192292081,21.6147847104095));
#204796=CARTESIAN_POINT('Ctrl Pts',(17.3280304725231,20.7936998097575,21.6184725799557));
#204797=CARTESIAN_POINT('Ctrl Pts',(17.3823193345552,20.8419265709082,21.62286614352));
#204798=CARTESIAN_POINT('Ctrl Pts',(17.4391954779977,20.8874483717554,21.6272597070843));
#204799=CARTESIAN_POINT('Ctrl Pts',(17.4983585908499,20.9299762383447,21.6316532706486));
#204800=CARTESIAN_POINT('Ctrl Pts',(17.5574354044305,20.9724420709446,21.6360404254673));
#204801=CARTESIAN_POINT('Ctrl Pts',(17.618792177104,21.011922361068,21.6404275802861));
#204802=CARTESIAN_POINT('Ctrl Pts',(17.6820942417089,21.0481671877306,21.6448147351048));
#204803=CARTESIAN_POINT('Ctrl Pts',(17.7453238390215,21.0843705218375,21.6491968675719));
#204804=CARTESIAN_POINT('Ctrl Pts',(17.8104938888271,21.1173455129229,21.6535790000389));
#204805=CARTESIAN_POINT('Ctrl Pts',(17.877240743402,21.1468854760118,21.657961132506));
#204806=CARTESIAN_POINT('Ctrl Pts',(17.9439464566845,21.1764072313176,21.662340563923));
#204807=CARTESIAN_POINT('Ctrl Pts',(18.0122266074123,21.2024979658372,21.6667199953401));
#204808=CARTESIAN_POINT('Ctrl Pts',(18.0816942022227,21.2249975536693,21.6710994267571));
#204809=CARTESIAN_POINT('Ctrl Pts',(18.1511417219742,21.2474906394691,21.6754775925863));
#204810=CARTESIAN_POINT('Ctrl Pts',(18.2217755472184,21.2663944910457,21.6798557584155));
#204811=CARTESIAN_POINT('Ctrl Pts',(18.293191587477,21.2815982090809,21.6842339242447));
#204812=CARTESIAN_POINT('Ctrl Pts',(18.3646103699648,21.2968025109076,21.6886122581865));
#204813=CARTESIAN_POINT('Ctrl Pts',(18.4368109563362,21.3083062989017,21.6929905921282));
#204814=CARTESIAN_POINT('Ctrl Pts',(18.5093787087695,21.3160497085641,21.69736892607));
#204815=CARTESIAN_POINT('Ctrl Pts',(18.5820224137337,21.3238012228122,21.7017518425644));
#204816=CARTESIAN_POINT('Ctrl Pts',(18.6550335728178,21.3277844496845,21.7061347590588));
#204817=CARTESIAN_POINT('Ctrl Pts',(18.7279928778285,21.3279914771872,21.7105176755531));
#204818=CARTESIAN_POINT('Ctrl Pts',(18.8009925375781,21.3281986191995,21.7149030162955));
#204819=CARTESIAN_POINT('Ctrl Pts',(18.8739398055028,21.324625426611,21.7192883570379));
#204820=CARTESIAN_POINT('Ctrl Pts',(18.9464185362624,21.3173160649466,21.7236736977803));
#204821=CARTESIAN_POINT('Ctrl Pts',(19.0190253583242,21.3099937854836,21.7280667887137));
#204822=CARTESIAN_POINT('Ctrl Pts',(19.0911615138916,21.2989222240549,21.7324598796471));
#204823=CARTESIAN_POINT('Ctrl Pts',(19.1624196844615,21.2841969452915,21.7368529705805));
#204824=CARTESIAN_POINT('Ctrl Pts',(19.2099750592608,21.2743697753681,21.7397847759327));
#204825=CARTESIAN_POINT('Ctrl Pts',(19.2571396374613,21.2629163751623,21.7427165812849));
#204826=CARTESIAN_POINT('Ctrl Pts',(19.3037966250894,21.2498773396251,21.7456483866371));
#204827=CARTESIAN_POINT('Ctrl Pts',(19.3728942477398,21.2305669125471,21.7499903038977));
#204828=CARTESIAN_POINT('Ctrl Pts',(19.4411602368598,21.2076975140762,21.7543322211583));
#204829=CARTESIAN_POINT('Ctrl Pts',(19.5081959039851,21.1813577599646,21.7586741384189));
#204830=CARTESIAN_POINT('Ctrl Pts',(19.5751306276509,21.1550576687074,21.7630095175459));
#204831=CARTESIAN_POINT('Ctrl Pts',(19.6408382497924,21.1252977672376,21.7673448966729));
#204832=CARTESIAN_POINT('Ctrl Pts',(19.7049335619748,21.0922168982419,21.7716802757999));
#204833=CARTESIAN_POINT('Ctrl Pts',(19.7689552079216,21.0591740498597,21.7760106721746));
#204834=CARTESIAN_POINT('Ctrl Pts',(19.8313677860799,21.0228180350837,21.7803410685494));
#204835=CARTESIAN_POINT('Ctrl Pts',(19.8918061585171,20.9833357185646,21.7846714649241));
#204836=CARTESIAN_POINT('Ctrl Pts',(19.9522073873422,20.9438776666937,21.7889991999671));
#204837=CARTESIAN_POINT('Ctrl Pts',(20.0106364037878,20.9012973912839,21.79332693501));
#204838=CARTESIAN_POINT('Ctrl Pts',(20.0667541884382,20.8558268216443,21.797654670053));
#204839=CARTESIAN_POINT('Ctrl Pts',(20.1228569262381,20.8103684440195,21.8019812447012));
#204840=CARTESIAN_POINT('Ctrl Pts',(20.1766492784224,20.7620216199763,21.8063078193494));
#204841=CARTESIAN_POINT('Ctrl Pts',(20.2278241391937,20.7110594792081,21.8106343939976));
#204842=CARTESIAN_POINT('Ctrl Pts',(20.2790030075947,20.6600933474689,21.8149613074705));
#204843=CARTESIAN_POINT('Ctrl Pts',(20.3275636296709,20.6065118422404,21.8192882209435));
#204844=CARTESIAN_POINT('Ctrl Pts',(20.3732360242913,20.550624670072,21.8236151344164));
#204845=CARTESIAN_POINT('Ctrl Pts',(20.4189632278337,20.4946704307904,21.8279472403796));
#204846=CARTESIAN_POINT('Ctrl Pts',(20.4617949724119,20.436405384436,21.8322793463428));
#204847=CARTESIAN_POINT('Ctrl Pts',(20.5015024142213,20.3761713246222,21.836611452306));
#204848=CARTESIAN_POINT('Ctrl Pts',(20.541234362149,20.3159000903411,21.8409462319015));
#204849=CARTESIAN_POINT('Ctrl Pts',(20.5778379231948,20.253657851612,21.845281011497));
#204850=CARTESIAN_POINT('Ctrl Pts',(20.6111298851782,20.1898117255995,21.8496157910926));
#204851=CARTESIAN_POINT('Ctrl Pts',(20.6444888929844,20.1258370215219,21.8539593003889));
#204852=CARTESIAN_POINT('Ctrl Pts',(20.6745227819993,20.0602524303901,21.8583028096851));
#204853=CARTESIAN_POINT('Ctrl Pts',(20.7010964440932,19.9934452566384,21.8626463189814));
#204854=CARTESIAN_POINT('Ctrl Pts',(20.7218525789006,19.9412635626139,21.8660389437605));
#204855=CARTESIAN_POINT('Ctrl Pts',(20.7404986559915,19.8883364226189,21.8694315685395));
#204856=CARTESIAN_POINT('Ctrl Pts',(20.7569919001287,19.8348531654274,21.8728241933186));
#204857=CARTESIAN_POINT('Ctrl Pts',(20.7789190860527,19.7637490627714,21.8773345682141));
#204858=CARTESIAN_POINT('Ctrl Pts',(20.7971283710036,19.6913742316258,21.8818449431095));
#204859=CARTESIAN_POINT('Ctrl Pts',(20.8114804792732,19.6181410790364,21.886355318005));
#204860=CARTESIAN_POINT('Ctrl Pts',(20.8265479701327,19.54125761101,21.8910905130881));
#204861=CARTESIAN_POINT('Ctrl Pts',(20.8373635164913,19.4634284696821,21.8958257081712));
#204862=CARTESIAN_POINT('Ctrl Pts',(20.8438247940449,19.3851503328552,21.9005609032544));
#204863=CARTESIAN_POINT('Ctrl Pts',(20.8499588376022,19.3108366237006,21.9050562824811));
#204864=CARTESIAN_POINT('Ctrl Pts',(20.8521688454906,19.2361188075755,21.9095516617078));
#204865=CARTESIAN_POINT('Ctrl Pts',(20.8504196160406,19.1614317759201,21.9140470409345));
#204866=CARTESIAN_POINT('Ctrl Pts',(20.8486720313618,19.0868149712324,21.9185381932313));
#204867=CARTESIAN_POINT('Ctrl Pts',(20.8429726196327,19.0122293415783,21.923029345528));
#204868=CARTESIAN_POINT('Ctrl Pts',(20.8333381899733,18.9381114437731,21.9275204978248));
#204869=CARTESIAN_POINT('Ctrl Pts',(20.823710302195,18.8640438728158,21.9320086005809));
#204870=CARTESIAN_POINT('Ctrl Pts',(20.8101527670998,18.7904438474655,21.9364967033371));
#204871=CARTESIAN_POINT('Ctrl Pts',(20.7927342525461,18.7177431932619,21.9409848060932));
#204872=CARTESIAN_POINT('Ctrl Pts',(20.7753230186655,18.6450729268217,21.945471032891));
#204873=CARTESIAN_POINT('Ctrl Pts',(20.7540541207903,18.5733017207355,21.9499572596887));
#204874=CARTESIAN_POINT('Ctrl Pts',(20.7290471325623,18.502850341485,21.9544434864864));
#204875=CARTESIAN_POINT('Ctrl Pts',(20.7040370351564,18.432390202848,21.9589302710673));
#204876=CARTESIAN_POINT('Ctrl Pts',(20.6752880624039,18.3632506455487,21.9634170556482));
#204877=CARTESIAN_POINT('Ctrl Pts',(20.6429691045691,18.2958355569623,21.9679038402291));
#204878=CARTESIAN_POINT('Ctrl Pts',(20.6106485910926,18.228417223416,21.9723908407771));
#204879=CARTESIAN_POINT('Ctrl Pts',(20.5747579519087,18.1627239264085,21.976877841325));
#204880=CARTESIAN_POINT('Ctrl Pts',(20.5355127633241,18.099136355671,21.9813648418729));
#204881=CARTESIAN_POINT('Ctrl Pts',(20.4962404866784,18.0355048951203,21.9858549394666));
#204882=CARTESIAN_POINT('Ctrl Pts',(20.4536092807961,17.9739824418484,21.9903450370603));
#204883=CARTESIAN_POINT('Ctrl Pts',(20.4078784777144,17.914921359699,21.994835134654));
#204884=CARTESIAN_POINT('Ctrl Pts',(20.3903440822918,17.892275783879,21.996556756436));
#204885=CARTESIAN_POINT('Ctrl Pts',(20.3723544291116,17.8699917351007,21.998278378218));
#204886=CARTESIAN_POINT('Ctrl Pts',(20.3539256943888,17.8480877707428,22.));
#204887=CARTESIAN_POINT('Origin',(18.734,-18.952,0.));
#204888=CARTESIAN_POINT('',(17.1140599642913,-20.3148951833168,21.9999997809128));
#204889=CARTESIAN_POINT('Ctrl Pts',(17.1140599642913,-20.3148951833168,
21.9999997809128));
#204890=CARTESIAN_POINT('Ctrl Pts',(17.1607068994597,-20.3703398270043,
21.9956147572469));
#204891=CARTESIAN_POINT('Ctrl Pts',(17.210295274204,-20.4234957880638,21.9912297335811));
#204892=CARTESIAN_POINT('Ctrl Pts',(17.2625717073312,-20.4740340927633,
21.9868447099152));
#204893=CARTESIAN_POINT('Ctrl Pts',(17.3147705210273,-20.5244973587843,
21.9824661970807));
#204894=CARTESIAN_POINT('Ctrl Pts',(17.3696491258074,-20.5723503507068,
21.9780876842462));
#204895=CARTESIAN_POINT('Ctrl Pts',(17.4269143804502,-20.6172976260014,
21.9737091714118));
#204896=CARTESIAN_POINT('Ctrl Pts',(17.4841122416856,-20.6621920044732,
21.9693358114907));
#204897=CARTESIAN_POINT('Ctrl Pts',(17.5436907950378,-20.7041871625307,
21.9649624515697));
#204898=CARTESIAN_POINT('Ctrl Pts',(17.605321866596,-20.7430261503327,21.9605890916486));
#204899=CARTESIAN_POINT('Ctrl Pts',(17.6669139416705,-20.7818405631288,
21.9562184989301));
#204900=CARTESIAN_POINT('Ctrl Pts',(17.7305555504131,-20.8175025110335,
21.9518479062116));
#204901=CARTESIAN_POINT('Ctrl Pts',(17.7958885836047,-20.8497976631951,
21.9474773134931));
#204902=CARTESIAN_POINT('Ctrl Pts',(17.8612019143776,-20.8820830761394,
21.94310803881));
#204903=CARTESIAN_POINT('Ctrl Pts',(17.9282052240273,-20.9110034951629,
21.9387387641268));
#204904=CARTESIAN_POINT('Ctrl Pts',(17.9965162832812,-20.9363907799561,
21.9343694894437));
#204905=CARTESIAN_POINT('Ctrl Pts',(18.0648293641575,-20.9617788160697,
21.9300000854546));
#204906=CARTESIAN_POINT('Ctrl Pts',(18.1344498178311,-20.9836333441171,
21.9256306814655));
#204907=CARTESIAN_POINT('Ctrl Pts',(18.2049775379727,-21.0018351725616,
21.9212612774765));
#204908=CARTESIAN_POINT('Ctrl Pts',(18.2755770529193,-21.0200555298444,
21.9168874255837));
#204909=CARTESIAN_POINT('Ctrl Pts',(18.347085209244,-21.0346156438901,21.912513573691));
#204910=CARTESIAN_POINT('Ctrl Pts',(18.4190897657556,-21.0454470483793,
21.9081397217982));
#204911=CARTESIAN_POINT('Ctrl Pts',(18.4911341450163,-21.0562844432714,
21.9037634509084));
#204912=CARTESIAN_POINT('Ctrl Pts',(18.5636749899472,-21.0633889762076,
21.8993871800187));
#204913=CARTESIAN_POINT('Ctrl Pts',(18.6362956526055,-21.0667441595853,
21.8950109091289));
#204914=CARTESIAN_POINT('Ctrl Pts',(18.7090404529568,-21.0701050783104,
21.8906271574457));
#204915=CARTESIAN_POINT('Ctrl Pts',(18.7818648602089,-21.0697038545041,
21.8862434057626));
#204916=CARTESIAN_POINT('Ctrl Pts',(18.8543536318168,-21.0655761172261,
21.8818596540794));
#204917=CARTESIAN_POINT('Ctrl Pts',(18.896359511156,-21.063184171133,21.8793193524552));
#204918=CARTESIAN_POINT('Ctrl Pts',(18.9382527891111,-21.0595418376991,
21.8767790508309));
#204919=CARTESIAN_POINT('Ctrl Pts',(18.979954172718,-21.054663916303,21.8742387492067));
#204920=CARTESIAN_POINT('Ctrl Pts',(19.0521148572584,-21.0462230897252,
21.8698429740959));
#204921=CARTESIAN_POINT('Ctrl Pts',(19.1239758615628,-21.0340474581782,
21.8654471989851));
#204922=CARTESIAN_POINT('Ctrl Pts',(19.1951213386526,-21.0181694294126,
21.8610514238743));
#204923=CARTESIAN_POINT('Ctrl Pts',(19.2661639899332,-21.0023143489949,
21.856662001931));
#204924=CARTESIAN_POINT('Ctrl Pts',(19.3364927019385,-20.9827675991443,
21.8522725799877));
#204925=CARTESIAN_POINT('Ctrl Pts',(19.4056979906368,-20.959613212094,21.8478831580444));
#204926=CARTESIAN_POINT('Ctrl Pts',(19.4748252628419,-20.936484927443,21.8434986843834));
#204927=CARTESIAN_POINT('Ctrl Pts',(19.5428311742357,-20.9097572368777,
21.8391142107225));
#204928=CARTESIAN_POINT('Ctrl Pts',(19.6093192887935,-20.8795645625156,
21.8347297370615));
#204929=CARTESIAN_POINT('Ctrl Pts',(19.675767120119,-20.8493901810247,21.8303479198267));
#204930=CARTESIAN_POINT('Ctrl Pts',(19.7406985429898,-20.8157551798471,
21.825966102592));
#204931=CARTESIAN_POINT('Ctrl Pts',(19.803736398282,-20.7788423681836,21.8215842853572));
#204932=CARTESIAN_POINT('Ctrl Pts',(19.8667566475552,-20.7419398660025,
21.8172036919325));
#204933=CARTESIAN_POINT('Ctrl Pts',(19.9278839650038,-20.7017616137434,
21.8128230985077));
#204934=CARTESIAN_POINT('Ctrl Pts',(19.9867666083377,-20.6585359137838,
21.808442505083));
#204935=CARTESIAN_POINT('Ctrl Pts',(20.0456520352798,-20.6153081703798,
21.8040617045708));
#204936=CARTESIAN_POINT('Ctrl Pts',(20.1022921913093,-20.5690329791144,
21.7996809040586));
#204937=CARTESIAN_POINT('Ctrl Pts',(20.1563664498668,-20.519980447038,21.7953001035464));
#204938=CARTESIAN_POINT('Ctrl Pts',(20.2104978279948,-20.4708760999272,
21.7909146755192));
#204939=CARTESIAN_POINT('Ctrl Pts',(20.2620575407503,-20.4189888782294,
21.786529247492));
#204940=CARTESIAN_POINT('Ctrl Pts',(20.3107606627202,-20.364626919076,21.7821438194648));
#204941=CARTESIAN_POINT('Ctrl Pts',(20.3594910299654,-20.3102345490068,
21.7777559381617));
#204942=CARTESIAN_POINT('Ctrl Pts',(20.4053613227915,-20.2533650591673,
21.7733680568587));
#204943=CARTESIAN_POINT('Ctrl Pts',(20.4481276167033,-20.1943588505964,
21.7689801755556));
#204944=CARTESIAN_POINT('Ctrl Pts',(20.4909696471634,-20.1352481455596,
21.7645845235772));
#204945=CARTESIAN_POINT('Ctrl Pts',(20.5306964397318,-20.0739935686515,
21.7601888715988));
#204946=CARTESIAN_POINT('Ctrl Pts',(20.5671083269304,-20.0109631068826,
21.7557932196204));
#204947=CARTESIAN_POINT('Ctrl Pts',(20.5912144107273,-19.969234492684,21.7528831272554));
#204948=CARTESIAN_POINT('Ctrl Pts',(20.613868534761,-19.9267280374392,21.7499730348904));
#204949=CARTESIAN_POINT('Ctrl Pts',(20.6350243858782,-19.8835553039387,
21.7470629425253));
#204950=CARTESIAN_POINT('Ctrl Pts',(20.6668849852277,-19.8185373967291,
21.7426803588893));
#204951=CARTESIAN_POINT('Ctrl Pts',(20.6954698819653,-19.7517530160599,
21.7382977752533));
#204952=CARTESIAN_POINT('Ctrl Pts',(20.7205800139613,-19.6835660244499,
21.7339151916173));
#204953=CARTESIAN_POINT('Ctrl Pts',(20.7456523661794,-19.6154816244714,
21.7295392018549));
#204954=CARTESIAN_POINT('Ctrl Pts',(20.7672601652298,-19.5459992525245,
21.7251632120926));
#204955=CARTESIAN_POINT('Ctrl Pts',(20.7852510275153,-19.4755057039971,
21.7207872223302));
#204956=CARTESIAN_POINT('Ctrl Pts',(20.8032203357683,-19.4050966105787,
21.7164164752418));
#204957=CARTESIAN_POINT('Ctrl Pts',(20.8175811957868,-19.3336792133251,
21.7120457281534));
#204958=CARTESIAN_POINT('Ctrl Pts',(20.8282305507602,-19.2616569073388,
21.707674981065));
#204959=CARTESIAN_POINT('Ctrl Pts',(20.8388730093072,-19.1896812423493,
21.7033070644331));
#204960=CARTESIAN_POINT('Ctrl Pts',(20.845808660676,-19.1171019231659,21.6989391478011));
#204961=CARTESIAN_POINT('Ctrl Pts',(20.8489855053725,-19.0443326164712,
21.6945712311692));
#204962=CARTESIAN_POINT('Ctrl Pts',(20.8521613481799,-18.9715862592065,
21.6902046920575));
#204963=CARTESIAN_POINT('Ctrl Pts',(20.8515807164049,-18.8986505164049,
21.6858381529459));
#204964=CARTESIAN_POINT('Ctrl Pts',(20.8472436019355,-18.8259425572265,
21.6814716138342));
#204965=CARTESIAN_POINT('Ctrl Pts',(20.8429064144311,-18.753233373679,21.677105001192));
#204966=CARTESIAN_POINT('Ctrl Pts',(20.8348126494595,-18.6807524641984,
21.6727383885499));
#204967=CARTESIAN_POINT('Ctrl Pts',(20.8230143052733,-18.6089136663121,
21.6683717759077));
#204968=CARTESIAN_POINT('Ctrl Pts',(20.8112037490663,-18.5370005107965,
21.6640006435495));
#204969=CARTESIAN_POINT('Ctrl Pts',(20.7956810363731,-18.4657312722987,
21.6596295111913));
#204970=CARTESIAN_POINT('Ctrl Pts',(20.7765494969166,-18.3955105098514,
21.6552583788331));
#204971=CARTESIAN_POINT('Ctrl Pts',(20.7574075807255,-18.3252516604421,
21.6508848756213));
#204972=CARTESIAN_POINT('Ctrl Pts',(20.734653092167,-18.2560428791505,21.6465113724094));
#204973=CARTESIAN_POINT('Ctrl Pts',(20.7084387230319,-18.1882718225755,
21.6421378691975));
#204974=CARTESIAN_POINT('Ctrl Pts',(20.6821776179286,-18.1203799411991,
21.6377565687388));
#204975=CARTESIAN_POINT('Ctrl Pts',(20.6524445121555,-18.0539313451297,
21.6333752682801));
#204976=CARTESIAN_POINT('Ctrl Pts',(20.619439293294,-17.9892914920377,21.6289939678214));
#204977=CARTESIAN_POINT('Ctrl Pts',(20.5965714267485,-17.9445053768408,
21.6259583571622));
#204978=CARTESIAN_POINT('Ctrl Pts',(20.57213375941,-17.9005870397827,21.622922746503));
#204979=CARTESIAN_POINT('Ctrl Pts',(20.546204814931,-17.8576496407728,21.6198871358438));
#204980=CARTESIAN_POINT('Ctrl Pts',(20.5087128672688,-17.7955643245834,
21.6154977957359));
#204981=CARTESIAN_POINT('Ctrl Pts',(20.4679537715697,-17.7352871414802,
21.6111084556279));
#204982=CARTESIAN_POINT('Ctrl Pts',(20.4241273153556,-17.6771828923768,
21.60671911552));
#204983=CARTESIAN_POINT('Ctrl Pts',(20.3803658454572,-17.6191648008458,
21.6023362839703));
#204984=CARTESIAN_POINT('Ctrl Pts',(20.3335463321389,-17.5633136287167,
21.5979534524206));
#204985=CARTESIAN_POINT('Ctrl Pts',(20.283913029103,-17.5099671979401,21.5935706208709));
#204986=CARTESIAN_POINT('Ctrl Pts',(20.2343380255226,-17.456683428072,21.5891929374108));
#204987=CARTESIAN_POINT('Ctrl Pts',(20.1819561246821,-17.4058989062031,
21.5848152539507));
#204988=CARTESIAN_POINT('Ctrl Pts',(20.1270521542449,-17.3579188554049,
21.5804375704906));
#204989=CARTESIAN_POINT('Ctrl Pts',(20.0721829959018,-17.3099692265604,
21.5760626627192));
#204990=CARTESIAN_POINT('Ctrl Pts',(20.0147953030245,-17.2648208570169,
21.5716877549478));
#204991=CARTESIAN_POINT('Ctrl Pts',(19.9552100903752,-17.222741512912,21.5673128471764));
#204992=CARTESIAN_POINT('Ctrl Pts',(19.8956430300011,-17.1806749880252,
21.5629392721942));
#204993=CARTESIAN_POINT('Ctrl Pts',(19.8338801725247,-17.1416759102888,
21.558565697212));
#204994=CARTESIAN_POINT('Ctrl Pts',(19.7702735413081,-17.1059701661173,
21.5541921222299));
#204995=CARTESIAN_POINT('Ctrl Pts',(19.7066653353733,-17.0702635379739,
21.5498184389705));
#204996=CARTESIAN_POINT('Ctrl Pts',(19.6412136864337,-17.0378506395157,
21.5454447557111));
#204997=CARTESIAN_POINT('Ctrl Pts',(19.5742959011684,-17.0089117882917,
21.5410710724518));
#204998=CARTESIAN_POINT('Ctrl Pts',(19.5073088887682,-16.9799429995295,
21.5366928645722));
#204999=CARTESIAN_POINT('Ctrl Pts',(19.4388531552012,-16.9544556253366,
21.5323146566927));
#205000=CARTESIAN_POINT('Ctrl Pts',(19.3693259376834,-16.9325817786039,
21.5279364488132));
#205001=CARTESIAN_POINT('Ctrl Pts',(19.2997608500006,-16.9106960175991,
21.5235558562063));
#205002=CARTESIAN_POINT('Ctrl Pts',(19.2291235834203,-16.8924278236772,
21.5191752635995));
#205003=CARTESIAN_POINT('Ctrl Pts',(19.1578238533414,-16.8778586496242,
21.5147946709926));
#205004=CARTESIAN_POINT('Ctrl Pts',(19.0863981311614,-16.8632637307212,
21.5104063375421));
#205005=CARTESIAN_POINT('Ctrl Pts',(19.0143080848955,-16.8523809568344,
21.5060180040915));
#205006=CARTESIAN_POINT('Ctrl Pts',(18.9419702886576,-16.8452400803519,
21.5016296706409));
#205007=CARTESIAN_POINT('Ctrl Pts',(18.8929666311248,-16.8404026497993,
21.4986568901481));
#205008=CARTESIAN_POINT('Ctrl Pts',(18.8438493706969,-16.8372813203535,
21.4956841096553));
#205009=CARTESIAN_POINT('Ctrl Pts',(18.7947475232676,-16.8358717575684,
21.4927113291624));
#205010=CARTESIAN_POINT('Ctrl Pts',(18.7222522474693,-16.8337906415164,
21.488322236837));
#205011=CARTESIAN_POINT('Ctrl Pts',(18.6495090698324,-16.8354351543627,
21.4839331445116));
#205012=CARTESIAN_POINT('Ctrl Pts',(18.5769328482517,-16.8408347033352,
21.4795440521862));
#205013=CARTESIAN_POINT('Ctrl Pts',(18.5044639925059,-16.8462262644699,
21.4751614528767));
#205014=CARTESIAN_POINT('Ctrl Pts',(18.4321620793838,-16.8553617985987,
21.4707788535672));
#205015=CARTESIAN_POINT('Ctrl Pts',(18.3604433407868,-16.868218720125,21.4663962542577));
#205016=CARTESIAN_POINT('Ctrl Pts',(18.2888084465286,-16.8810606109898,
21.4620187785205));
#205017=CARTESIAN_POINT('Ctrl Pts',(18.2177558446894,-16.8976151620993,
21.4576413027833));
#205018=CARTESIAN_POINT('Ctrl Pts',(18.1476963106892,-16.917808026783,21.4532638270461));
#205019=CARTESIAN_POINT('Ctrl Pts',(18.0776809567047,-16.9379881577097,
21.4488891117746));
#205020=CARTESIAN_POINT('Ctrl Pts',(18.0086578901714,-16.9618019166529,
21.4445143965032));
#205021=CARTESIAN_POINT('Ctrl Pts',(17.9410259673652,-16.9891242567175,
21.4401396812318));
#205022=CARTESIAN_POINT('Ctrl Pts',(17.8734144087345,-17.0164383699432,
21.4357662832003));
#205023=CARTESIAN_POINT('Ctrl Pts',(17.8071936089994,-17.0472587863894,
21.4313928851688));
#205024=CARTESIAN_POINT('Ctrl Pts',(17.7427439831315,-17.0814117211363,
21.4270194871373));
#205025=CARTESIAN_POINT('Ctrl Pts',(17.6782925274241,-17.1155656255459,
21.4226459649373));
#205026=CARTESIAN_POINT('Ctrl Pts',(17.6156127705188,-17.1530520085839,
21.4182724427373));
#205027=CARTESIAN_POINT('Ctrl Pts',(17.5550604851453,-17.1936511664877,
21.4138989205372));
#205028=CARTESIAN_POINT('Ctrl Pts',(17.4944451983905,-17.2342925656217,
21.4095208479236));
#205029=CARTESIAN_POINT('Ctrl Pts',(17.4359622039086,-17.2780529367419,
21.4051427753101));
#205030=CARTESIAN_POINT('Ctrl Pts',(17.3799375208465,-17.32466973157,21.4007647026965));
#205031=CARTESIAN_POINT('Ctrl Pts',(17.3238821391245,-17.3713120700164,
21.3963842311231));
#205032=CARTESIAN_POINT('Ctrl Pts',(17.2702881051855,-17.4208136210668,
21.3920037595497));
#205033=CARTESIAN_POINT('Ctrl Pts',(17.2194455841251,-17.4728739332451,
21.3876232879764));
#205034=CARTESIAN_POINT('Ctrl Pts',(17.1685129338239,-17.5250265334593,
21.3832350510804));
#205035=CARTESIAN_POINT('Ctrl Pts',(17.120341855727,-17.5797465906982,21.3788468141844));
#205036=CARTESIAN_POINT('Ctrl Pts',(17.0751827470182,-17.6366999121075,
21.3744585772885));
#205037=CARTESIAN_POINT('Ctrl Pts',(17.0445738554429,-17.6753029335071,
21.371484225686));
#205038=CARTESIAN_POINT('Ctrl Pts',(17.015347839445,-17.7149312818909,21.3685098740835));
#205039=CARTESIAN_POINT('Ctrl Pts',(16.9875709599417,-17.7554739417626,
21.365535522481));
#205040=CARTESIAN_POINT('Ctrl Pts',(16.9460065706275,-17.8161406159491,
21.3610848026675));
#205041=CARTESIAN_POINT('Ctrl Pts',(16.9075294243376,-17.8790885067208,
21.3566340828539));
#205042=CARTESIAN_POINT('Ctrl Pts',(16.8723942159318,-17.9439757419964,
21.3521833630404));
#205043=CARTESIAN_POINT('Ctrl Pts',(16.8373241044052,-18.0087427572218,
21.3477408893134));
#205044=CARTESIAN_POINT('Ctrl Pts',(16.8055838426314,-18.0754415697969,
21.3432984155865));
#205045=CARTESIAN_POINT('Ctrl Pts',(16.777385030688,-18.1437012545698,21.3388559418595));
#205046=CARTESIAN_POINT('Ctrl Pts',(16.7661659391973,-18.1708588401492,
21.3370884730992));
#205047=CARTESIAN_POINT('Ctrl Pts',(16.7555069377213,-18.1982631828448,
21.3353210043389));
#205048=CARTESIAN_POINT('Ctrl Pts',(16.7454193692319,-18.2258897639242,
21.3335535355786));
#205049=CARTESIAN_POINT('',(20.3539256943886,-20.3149122292574,22.));
#205050=CARTESIAN_POINT('Origin',(18.734,-18.952,22.));
#205051=CARTESIAN_POINT('Ctrl Pts',(16.7454193692319,-18.2258897639242,
21.5555703664997));
#205052=CARTESIAN_POINT('Ctrl Pts',(16.7701108597548,-18.1582677729935,
21.5598847303809));
#205053=CARTESIAN_POINT('Ctrl Pts',(16.7982600389245,-18.0918947722405,
21.5641990942621));
#205054=CARTESIAN_POINT('Ctrl Pts',(16.8297061728116,-18.0271464874196,
21.5685134581433));
#205055=CARTESIAN_POINT('Ctrl Pts',(16.861178996372,-17.9623432479715,21.572831483809));
#205056=CARTESIAN_POINT('Ctrl Pts',(16.8959541479334,-17.8991679273281,
21.5771495094746));
#205057=CARTESIAN_POINT('Ctrl Pts',(16.9338240950207,-17.8379731999939,
21.5814675351402));
#205058=CARTESIAN_POINT('Ctrl Pts',(16.9717095113551,-17.7767534756255,
21.5857873246479));
#205059=CARTESIAN_POINT('Ctrl Pts',(17.0126919573595,-17.7175163644594,
21.5901071141556));
#205060=CARTESIAN_POINT('Ctrl Pts',(17.0565211557699,-17.6605846031735,
21.5944269036633));
#205061=CARTESIAN_POINT('Ctrl Pts',(17.1004271278893,-17.6035531169866,
21.5987542599592));
#205062=CARTESIAN_POINT('Ctrl Pts',(17.1471894885155,-17.5488354241871,
21.6030816162551));
#205063=CARTESIAN_POINT('Ctrl Pts',(17.1965188161309,-17.4967197488976,
21.607408972551));
#205064=CARTESIAN_POINT('Ctrl Pts',(17.2385583646031,-17.45230561306,21.6110968416859));
#205065=CARTESIAN_POINT('Ctrl Pts',(17.2824614873855,-17.4097807692747,
21.6147847108208));
#205066=CARTESIAN_POINT('Ctrl Pts',(17.3280304696825,-17.3693001927659,
21.6184725799558));
#205067=CARTESIAN_POINT('Ctrl Pts',(17.3823193529476,-17.3210734125788,
21.6228661452028));
#205068=CARTESIAN_POINT('Ctrl Pts',(17.4391955190593,-17.2755515953447,
21.6272597104498));
#205069=CARTESIAN_POINT('Ctrl Pts',(17.4983586556721,-17.2330237150596,
21.6316532756968));
#205070=CARTESIAN_POINT('Ctrl Pts',(17.5574354931409,-17.1905578686671,
21.6360404322079));
#205071=CARTESIAN_POINT('Ctrl Pts',(17.6187922908035,-17.1510775674503,
21.640427588719));
#205072=CARTESIAN_POINT('Ctrl Pts',(17.6820943811751,-17.1148327324153,
21.64481474523));
#205073=CARTESIAN_POINT('Ctrl Pts',(17.7453240043386,-17.0786293898806,
21.6491968793954));
#205074=CARTESIAN_POINT('Ctrl Pts',(17.810494080778,-17.0456543930935,21.6535790135607));
#205075=CARTESIAN_POINT('Ctrl Pts',(17.8772409624661,-17.0161144270376,
21.6579611477261));
#205076=CARTESIAN_POINT('Ctrl Pts',(17.9439467029022,-16.9865926687415,
21.6623405808441));
#205077=CARTESIAN_POINT('Ctrl Pts',(18.0122268812651,-16.9605019339683,
21.6667200139621));
#205078=CARTESIAN_POINT('Ctrl Pts',(18.0816945039053,-16.9380023486199,
21.6710994470801));
#205079=CARTESIAN_POINT('Ctrl Pts',(18.1511420514884,-16.9155092652999,
21.6754776146104));
#205080=CARTESIAN_POINT('Ctrl Pts',(18.2217759047592,-16.8966054189395,
21.6798557821407));
#205081=CARTESIAN_POINT('Ctrl Pts',(18.2931919729642,-16.881401708853,21.684233949671));
#205082=CARTESIAN_POINT('Ctrl Pts',(18.364610783359,-16.866197414984,21.6886122853114));
#205083=CARTESIAN_POINT('Ctrl Pts',(18.4368113975566,-16.8546936376761,
21.6929906209519));
#205084=CARTESIAN_POINT('Ctrl Pts',(18.5093791774671,-16.8469502414231,
21.6973689565923));
#205085=CARTESIAN_POINT('Ctrl Pts',(18.5820229096485,-16.8391987406294,
21.7017518747697));
#205086=CARTESIAN_POINT('Ctrl Pts',(18.6550340955975,-16.8352155299105,
21.7061347929472));
#205087=CARTESIAN_POINT('Ctrl Pts',(18.7279934268567,-16.835008521255,21.7105177111246));
#205088=CARTESIAN_POINT('Ctrl Pts',(18.8009931127498,-16.8348013981006,
21.7149030535438));
#205089=CARTESIAN_POINT('Ctrl Pts',(18.8739404062014,-16.8383746122317,
21.719288395963));
#205090=CARTESIAN_POINT('Ctrl Pts',(18.9464191616025,-16.845683998118,21.7236737383821));
#205091=CARTESIAN_POINT('Ctrl Pts',(19.019026007826,-16.8530063017931,21.7280668309636));
#205092=CARTESIAN_POINT('Ctrl Pts',(19.0911621866738,-16.8640778900689,
21.7324599235451));
#205093=CARTESIAN_POINT('Ctrl Pts',(19.1624203793687,-16.8788031983091,
21.7368530161266));
#205094=CARTESIAN_POINT('Ctrl Pts',(19.2099755048328,-16.8886303333286,
21.7397848062968));
#205095=CARTESIAN_POINT('Ctrl Pts',(19.2571398375277,-16.9000836817304,
21.742716596467));
#205096=CARTESIAN_POINT('Ctrl Pts',(19.3037965853284,-16.9131226492631,
21.7456483866372));
#205097=CARTESIAN_POINT('Ctrl Pts',(19.3728941566259,-16.932433060537,21.7499903005052));
#205098=CARTESIAN_POINT('Ctrl Pts',(19.4411600971652,-16.9553024383045,
21.7543322143732));
#205099=CARTESIAN_POINT('Ctrl Pts',(19.5081957188875,-16.9816421673066,
21.7586741282413));
#205100=CARTESIAN_POINT('Ctrl Pts',(19.5751303969638,-17.007942233392,21.7630095039643));
#205101=CARTESIAN_POINT('Ctrl Pts',(19.6408379766924,-17.0377021052713,
21.7673448796873));
#205102=CARTESIAN_POINT('Ctrl Pts',(19.7049332499917,-17.0707829407374,
21.7716802554104));
#205103=CARTESIAN_POINT('Ctrl Pts',(19.7689548569736,-17.1038257555634,
21.7760106483765));
#205104=CARTESIAN_POINT('Ctrl Pts',(19.8313673996942,-17.1401817328403,
21.7803410413427));
#205105=CARTESIAN_POINT('Ctrl Pts',(19.8918057405323,-17.1796640083804,
21.7846714343088));
#205106=CARTESIAN_POINT('Ctrl Pts',(19.9522069377095,-17.2191220192527,
21.7889991659403));
#205107=CARTESIAN_POINT('Ctrl Pts',(20.0106359263449,-17.2617022501812,
21.7933268975719));
#205108=CARTESIAN_POINT('Ctrl Pts',(20.0667536873044,-17.307172772302,21.7976546292034));
#205109=CARTESIAN_POINT('Ctrl Pts',(20.1228564014125,-17.3526311024149,
21.8019812004406));
#205110=CARTESIAN_POINT('Ctrl Pts',(20.1766487340221,-17.4009778759096,
21.8063077716777));
#205111=CARTESIAN_POINT('Ctrl Pts',(20.2278235795987,-17.4519399635232,
21.8106343429149));
#205112=CARTESIAN_POINT('Ctrl Pts',(20.2790024328481,-17.5029060421478,
21.8149612529802));
#205113=CARTESIAN_POINT('Ctrl Pts',(20.3275630441483,-17.5564874916594,
21.8192881630456));
#205114=CARTESIAN_POINT('Ctrl Pts',(20.3732354326212,-17.6123746059293,
21.823615073111));
#205115=CARTESIAN_POINT('Ctrl Pts',(20.4189626303271,-17.6683287876325,
21.8279471756927));
#205116=CARTESIAN_POINT('Ctrl Pts',(20.4617943736678,-17.7265937742531,
21.8322792782743));
#205117=CARTESIAN_POINT('Ctrl Pts',(20.5015018190868,-17.7868277725912,
21.836611380856));
#205118=CARTESIAN_POINT('Ctrl Pts',(20.5412337707152,-17.8470989454934,
21.8409461570777));
#205119=CARTESIAN_POINT('Ctrl Pts',(20.5778373403004,-17.9093411211074,
21.8452809332993));
#205120=CARTESIAN_POINT('Ctrl Pts',(20.6111293159145,-17.973187182688,21.8496157095209));
#205121=CARTESIAN_POINT('Ctrl Pts',(20.6444883378172,-18.0371618230444,
21.8539592154936));
#205122=CARTESIAN_POINT('Ctrl Pts',(20.674522245953,-18.1027463491743,21.8583027214662));
#205123=CARTESIAN_POINT('Ctrl Pts',(20.7010959324481,-18.1695534570681,
21.8626462274389));
#205124=CARTESIAN_POINT('Ctrl Pts',(20.7218522888838,-18.2217356089171,
21.8660388827321));
#205125=CARTESIAN_POINT('Ctrl Pts',(20.7404985496073,-18.2746632207694,
21.8694315380253));
#205126=CARTESIAN_POINT('Ctrl Pts',(20.7569919383483,-18.3281469585088,
21.8728241933186));
#205127=CARTESIAN_POINT('Ctrl Pts',(20.7789191314163,-18.3992510998001,
21.8773345707065));
#205128=CARTESIAN_POINT('Ctrl Pts',(20.7971284192367,-18.4716259697097,
21.8818449480945));
#205129=CARTESIAN_POINT('Ctrl Pts',(20.8114805262578,-18.5448591607076,
21.8863553254824));
#205130=CARTESIAN_POINT('Ctrl Pts',(20.8265480064888,-18.621742621512,21.891090520254));
#205131=CARTESIAN_POINT('Ctrl Pts',(20.8373635429458,-18.6995717540552,
21.8958257150255));
#205132=CARTESIAN_POINT('Ctrl Pts',(20.843824811693,-18.7778498809511,21.9005609097971));
#205133=CARTESIAN_POINT('Ctrl Pts',(20.8499588507186,-18.8521636270621,
21.9050562915339));
#205134=CARTESIAN_POINT('Ctrl Pts',(20.8521688501583,-18.9268814796183,
21.9095516732707));
#205135=CARTESIAN_POINT('Ctrl Pts',(20.8504196084828,-19.0015685467751,
21.9140470550075));
#205136=CARTESIAN_POINT('Ctrl Pts',(20.8486720115918,-19.0761853868609,
21.9185382098078));
#205137=CARTESIAN_POINT('Ctrl Pts',(20.8429725838885,-19.1507710509859,
21.9230293646081));
#205138=CARTESIAN_POINT('Ctrl Pts',(20.8333381346341,-19.2248889819521,
21.9275205194084));
#205139=CARTESIAN_POINT('Ctrl Pts',(20.8237102273003,-19.2989565858473,
21.9320086246542));
#205140=CARTESIAN_POINT('Ctrl Pts',(20.8101526690551,-19.3725566428308,
21.9364967299001));
#205141=CARTESIAN_POINT('Ctrl Pts',(20.7927341278966,-19.4452573269945,
21.9409848351459));
#205142=CARTESIAN_POINT('Ctrl Pts',(20.7753228675005,-19.5179276230559,
21.9454710644121));
#205143=CARTESIAN_POINT('Ctrl Pts',(20.7540539396924,-19.5896988571003,
21.9499572936783));
#205144=CARTESIAN_POINT('Ctrl Pts',(20.7290469182522,-19.6601502622835,
21.9544435229445));
#205145=CARTESIAN_POINT('Ctrl Pts',(20.7040367879202,-19.7306104260392,
21.9589303099422));
#205146=CARTESIAN_POINT('Ctrl Pts',(20.6752877790479,-19.7997500064623,
21.9634170969398));
#205147=CARTESIAN_POINT('Ctrl Pts',(20.6429687820359,-19.8671651158193,
21.9679038839375));
#205148=CARTESIAN_POINT('Ctrl Pts',(20.6106482296079,-19.9345834696624,
21.9723908868707));
#205149=CARTESIAN_POINT('Ctrl Pts',(20.5747575484645,-20.0002767846379,
21.9768778898039));
#205150=CARTESIAN_POINT('Ctrl Pts',(20.5355123150534,-20.0638643706455,
21.9813648927371));
#205151=CARTESIAN_POINT('Ctrl Pts',(20.4962399941625,-20.1274958454851,
21.9858549926477));
#205152=CARTESIAN_POINT('Ctrl Pts',(20.4536087412679,-20.1890183104101,
21.9903450925584));
#205153=CARTESIAN_POINT('Ctrl Pts',(20.407877888554,-20.2480794011981,21.994835192469));
#205154=CARTESIAN_POINT('Ctrl Pts',(20.3903436794274,-20.2707247151527,
21.9965567949793));
#205155=CARTESIAN_POINT('Ctrl Pts',(20.372354222822,-20.2930085100904,21.9982783974897));
#205156=CARTESIAN_POINT('Ctrl Pts',(20.3539256943887,-20.3149122292573,
22.));
#205157=CARTESIAN_POINT('Origin',(-18.734,-18.952,0.));
#205158=CARTESIAN_POINT('',(-20.3539401105369,-20.3148950943758,21.9999997808643));
#205159=CARTESIAN_POINT('Ctrl Pts',(-20.3539401105369,-20.3148950943758,
21.9999997808643));
#205160=CARTESIAN_POINT('Ctrl Pts',(-20.3072932296543,-20.3703396797185,
21.9956147616661));
#205161=CARTESIAN_POINT('Ctrl Pts',(-20.2577049138449,-20.4234955896159,
21.9912297424679));
#205162=CARTESIAN_POINT('Ctrl Pts',(-20.2054285432655,-20.4740338504986,
21.9868447232696));
#205163=CARTESIAN_POINT('Ctrl Pts',(-20.1532297926735,-20.5244970721403,
21.9824662149506));
#205164=CARTESIAN_POINT('Ctrl Pts',(-20.0983512546661,-20.5723500270703,
21.9780877066316));
#205165=CARTESIAN_POINT('Ctrl Pts',(-20.0410860694924,-20.6172972728431,
21.9737091983125));
#205166=CARTESIAN_POINT('Ctrl Pts',(-19.983888278367,-20.6621916212607,
21.9693358429569));
#205167=CARTESIAN_POINT('Ctrl Pts',(-19.9243097978752,-20.7041867567888,
21.9649624876012));
#205168=CARTESIAN_POINT('Ctrl Pts',(-19.8626788010172,-20.7430257296126,
21.9605891322455));
#205169=CARTESIAN_POINT('Ctrl Pts',(-19.8010868010387,-20.7818401271607,
21.956218544121));
#205170=CARTESIAN_POINT('Ctrl Pts',(-19.7374452692593,-20.8175020674031,
21.9518479559964));
#205171=CARTESIAN_POINT('Ctrl Pts',(-19.6721123140465,-20.8497972194717,
21.9474773678718));
#205172=CARTESIAN_POINT('Ctrl Pts',(-19.6067990615792,-20.8820826321498,
21.9431080978047));
#205173=CARTESIAN_POINT('Ctrl Pts',(-19.5397958312689,-20.911003058507,
21.9387388277375));
#205174=CARTESIAN_POINT('Ctrl Pts',(-19.4714848515874,-20.9363903581904,
21.9343695576704));
#205175=CARTESIAN_POINT('Ctrl Pts',(-19.4031718505269,-20.9617784091052,
21.9300001583129));
#205176=CARTESIAN_POINT('Ctrl Pts',(-19.3335514769124,-20.9836329595348,
21.9256307589554));
#205177=CARTESIAN_POINT('Ctrl Pts',(-19.2630238363122,-21.001834817885,
21.9212613595979));
#205178=CARTESIAN_POINT('Ctrl Pts',(-19.192424400798,-21.0200552051529,
21.9168875123296));
#205179=CARTESIAN_POINT('Ctrl Pts',(-19.1209163233831,-21.0346153567022,
21.9125136650614));
#205180=CARTESIAN_POINT('Ctrl Pts',(-19.0489118445282,-21.0454468061491,
21.9081398177931));
#205181=CARTESIAN_POINT('Ctrl Pts',(-18.9768675429743,-21.0562842460226,
21.9037635515308));
#205182=CARTESIAN_POINT('Ctrl Pts',(-18.904326774497,-21.0633888314031,
21.8993872852686));
#205183=CARTESIAN_POINT('Ctrl Pts',(-18.8317061863209,-21.0667440746234,
21.8950110190063));
#205184=CARTESIAN_POINT('Ctrl Pts',(-18.7589614597164,-21.0701050533332,
21.8906272719066));
#205185=CARTESIAN_POINT('Ctrl Pts',(-18.6861371242322,-21.0697038968461,
21.8862435248068));
#205186=CARTESIAN_POINT('Ctrl Pts',(-18.6136484217024,-21.0655762341589,
21.8818597777071));
#205187=CARTESIAN_POINT('Ctrl Pts',(-18.5716418570464,-21.063184289987,
21.8793194348736));
#205188=CARTESIAN_POINT('Ctrl Pts',(-18.5297478967642,-21.0595419177169,
21.8767790920401));
#205189=CARTESIAN_POINT('Ctrl Pts',(-18.4880458377735,-21.0546639175302,
21.8742387492067));
#205190=CARTESIAN_POINT('Ctrl Pts',(-18.4158851680032,-21.0462230930451,
21.8698429748793));
#205191=CARTESIAN_POINT('Ctrl Pts',(-18.3440241776343,-21.0340474650401,
21.8654472005519));
#205192=CARTESIAN_POINT('Ctrl Pts',(-18.2728787135213,-21.0181694410566,
21.8610514262245));
#205193=CARTESIAN_POINT('Ctrl Pts',(-18.2018360755882,-21.0023143655011,
21.8566620050875));
#205194=CARTESIAN_POINT('Ctrl Pts',(-18.1315073759669,-20.9827676217893,
21.8522725839506));
#205195=CARTESIAN_POINT('Ctrl Pts',(-18.0623020985936,-20.9596132419483,
21.8478831628136));
#205196=CARTESIAN_POINT('Ctrl Pts',(-17.9931748381961,-20.9364849646642,
21.8434986899895));
#205197=CARTESIAN_POINT('Ctrl Pts',(-17.9251689375377,-20.9097572825852,
21.8391142171653));
#205198=CARTESIAN_POINT('Ctrl Pts',(-17.8586808325707,-20.8795646176279,
21.8347297443412));
#205199=CARTESIAN_POINT('Ctrl Pts',(-17.7922330111159,-20.8493902456658,
21.8303479279616));
#205200=CARTESIAN_POINT('Ctrl Pts',(-17.7273015969599,-20.8157552549639,
21.8259661115821));
#205201=CARTESIAN_POINT('Ctrl Pts',(-17.6642637491768,-20.7788424545304,
21.8215842952025));
#205202=CARTESIAN_POINT('Ctrl Pts',(-17.6012435076605,-20.7419399637226,
21.8172037026501));
#205203=CARTESIAN_POINT('Ctrl Pts',(-17.5401161967491,-20.7017617236165,
21.8128231100976));
#205204=CARTESIAN_POINT('Ctrl Pts',(-17.4812335587017,-20.6585360364073,
21.8084425175452));
#205205=CARTESIAN_POINT('Ctrl Pts',(-17.4223481372602,-20.6153083059113,
21.8040617179213));
#205206=CARTESIAN_POINT('Ctrl Pts',(-17.3657079854645,-20.5690331281733,
21.7996809182973));
#205207=CARTESIAN_POINT('Ctrl Pts',(-17.3116337298584,-20.5199806100726,
21.7953001186734));
#205208=CARTESIAN_POINT('Ctrl Pts',(-17.2575023549029,-20.47087627715,21.790914691553));
#205209=CARTESIAN_POINT('Ctrl Pts',(-17.2059426440142,-20.4189890701121,
21.7865292644327));
#205210=CARTESIAN_POINT('Ctrl Pts',(-17.1572395226006,-20.3646271259293,
21.7821438373123));
#205211=CARTESIAN_POINT('Ctrl Pts',(-17.1085091560373,-20.3102347709788,
21.7777559569279));
#205212=CARTESIAN_POINT('Ctrl Pts',(-17.0626388625667,-20.253365296582,
21.7733680765434));
#205213=CARTESIAN_POINT('Ctrl Pts',(-17.0198725666879,-20.1943591036278,
21.768980196159));
#205214=CARTESIAN_POINT('Ctrl Pts',(-16.9770305343292,-20.1352484143348,
21.7645845451083));
#205215=CARTESIAN_POINT('Ctrl Pts',(-16.9373037385248,-20.0739938533524,
21.7601888940575));
#205216=CARTESIAN_POINT('Ctrl Pts',(-16.9008918467625,-20.010963407552,
21.7557932430068));
#205217=CARTESIAN_POINT('Ctrl Pts',(-16.8767856902822,-19.9692346833373,
21.7528831428463));
#205218=CARTESIAN_POINT('Ctrl Pts',(-16.8541315013796,-19.9267281135982,
21.7499730426858));
#205219=CARTESIAN_POINT('Ctrl Pts',(-16.8329755935997,-19.8835552620593,
21.7470629425253));
#205220=CARTESIAN_POINT('Ctrl Pts',(-16.8011149796973,-19.8185373215268,
21.7426803568856));
#205221=CARTESIAN_POINT('Ctrl Pts',(-16.7725300723094,-19.7517529070192,
21.7382977712459));
#205222=CARTESIAN_POINT('Ctrl Pts',(-16.7474199334088,-19.6835658815327,
21.7339151856062));
#205223=CARTESIAN_POINT('Ctrl Pts',(-16.722347574114,-19.6154814472323,
21.7295391938112));
#205224=CARTESIAN_POINT('Ctrl Pts',(-16.7007397717712,-19.5459990409051,
21.7251632020162));
#205225=CARTESIAN_POINT('Ctrl Pts',(-16.6827489097976,-19.4755054583704,
21.7207872102213));
#205226=CARTESIAN_POINT('Ctrl Pts',(-16.6647796017072,-19.4050963304016,
21.7164164610665));
#205227=CARTESIAN_POINT('Ctrl Pts',(-16.6504187455061,-19.3336788989525,
21.7120457119117));
#205228=CARTESIAN_POINT('Ctrl Pts',(-16.6397693978102,-19.2616565595166,
21.7076749627569));
#205229=CARTESIAN_POINT('Ctrl Pts',(-16.6291269464843,-19.1896808607495,
21.7033070440387));
#205230=CARTESIAN_POINT('Ctrl Pts',(-16.6221913058276,-19.117101508527,
21.6989391253204));
#205231=CARTESIAN_POINT('Ctrl Pts',(-16.6190144751312,-19.0443321698839,
21.6945712066022));
#205232=CARTESIAN_POINT('Ctrl Pts',(-16.6158386463066,-18.9715857803861,
21.6902046653873));
#205233=CARTESIAN_POINT('Ctrl Pts',(-16.6164192953802,-18.8986500064394,
21.6858381241723));
#205234=CARTESIAN_POINT('Ctrl Pts',(-16.6207564302585,-18.8259420175236,
21.6814715829573));
#205235=CARTESIAN_POINT('Ctrl Pts',(-16.6250936381862,-18.7532328040023,
21.6771049681976));
#205236=CARTESIAN_POINT('Ctrl Pts',(-16.6331874267156,-18.6807518659564,
21.6727383534379));
#205237=CARTESIAN_POINT('Ctrl Pts',(-16.64498579739,-18.6089130412075,21.6683717386782));
#205238=CARTESIAN_POINT('Ctrl Pts',(-16.6567963801275,-18.5369998587107,
21.6640006041948));
#205239=CARTESIAN_POINT('Ctrl Pts',(-16.672319122297,-18.465730594939,21.6596294697114));
#205240=CARTESIAN_POINT('Ctrl Pts',(-16.6914506939752,-18.3955098091991,
21.655258335228));
#205241=CARTESIAN_POINT('Ctrl Pts',(-16.7105926424343,-18.325250936379,
21.6508848298832));
#205242=CARTESIAN_POINT('Ctrl Pts',(-16.7333471660201,-18.2560421336627,
21.6465113245384));
#205243=CARTESIAN_POINT('Ctrl Pts',(-16.7595615727462,-18.1882710579117,
21.6421378191936));
#205244=CARTESIAN_POINT('Ctrl Pts',(-16.7858227154186,-18.1203791575545,
21.6377565166129));
#205245=CARTESIAN_POINT('Ctrl Pts',(-16.8155558613104,-18.0539305447508,
21.6333752140323));
#205246=CARTESIAN_POINT('Ctrl Pts',(-16.8485611226492,-17.9892906774244,
21.6289939114516));
#205247=CARTESIAN_POINT('Ctrl Pts',(-16.8714288660015,-17.9445048512745,
21.6259583195824));
#205248=CARTESIAN_POINT('Ctrl Pts',(-16.8958663903147,-17.9005867928719,
21.6229227277131));
#205249=CARTESIAN_POINT('Ctrl Pts',(-16.9217951734766,-17.8576496599694,
21.6198871358438));
#205250=CARTESIAN_POINT('Ctrl Pts',(-16.9592871125939,-17.7955643564438,
21.6154977965973));
#205251=CARTESIAN_POINT('Ctrl Pts',(-17.0000461986468,-17.7352871847913,
21.6111084573508));
#205252=CARTESIAN_POINT('Ctrl Pts',(-17.0438726443021,-17.6771829458619,
21.6067191181042));
#205253=CARTESIAN_POINT('Ctrl Pts',(-17.0876341035589,-17.6191648646202,
21.6023362874245));
#205254=CARTESIAN_POINT('Ctrl Pts',(-17.134453605312,-17.5633137014982,
21.5979534567447));
#205255=CARTESIAN_POINT('Ctrl Pts',(-17.1840868960386,-17.5099672783988,
21.593570626065));
#205256=CARTESIAN_POINT('Ctrl Pts',(-17.2336618872153,-17.4566835163159,
21.5891929434835));
#205257=CARTESIAN_POINT('Ctrl Pts',(-17.2860437748972,-17.4058990008948,
21.5848152609019));
#205258=CARTESIAN_POINT('Ctrl Pts',(-17.3409477315906,-17.3579189551721,
21.5804375783204));
#205259=CARTESIAN_POINT('Ctrl Pts',(-17.3958168761313,-17.3099693314588,
21.5760626714324));
#205260=CARTESIAN_POINT('Ctrl Pts',(-17.4532045546155,-17.2648209656694,
21.5716877645444));
#205261=CARTESIAN_POINT('Ctrl Pts',(-17.5127897524411,-17.2227416239159,
21.5673128576563));
#205262=CARTESIAN_POINT('Ctrl Pts',(-17.5723567979443,-17.1806751014162,
21.5629392835611));
#205263=CARTESIAN_POINT('Ctrl Pts',(-17.6341196401156,-17.14167602466,21.5585657094658));
#205264=CARTESIAN_POINT('Ctrl Pts',(-17.6977262557446,-17.1059702800424,
21.5541921353705));
#205265=CARTESIAN_POINT('Ctrl Pts',(-17.761334446059,-17.0702636514709,
21.5498184530003));
#205266=CARTESIAN_POINT('Ctrl Pts',(-17.8267860790938,-17.0378507511553,
21.5454447706301));
#205267=CARTESIAN_POINT('Ctrl Pts',(-17.8937038483149,-17.0089118966287,
21.5410710882598));
#205268=CARTESIAN_POINT('Ctrl Pts',(-17.9606908447099,-16.9799431045363,
21.5366928812667));
#205269=CARTESIAN_POINT('Ctrl Pts',(-18.0291465621343,-16.9544557255711,
21.5323146742736));
#205270=CARTESIAN_POINT('Ctrl Pts',(-18.0986737635119,-16.9325818726103,
21.5279364672805));
#205271=CARTESIAN_POINT('Ctrl Pts',(-18.168238835056,-16.9106961053709,
21.5235558755599));
#205272=CARTESIAN_POINT('Ctrl Pts',(-18.2388760855,-16.8924279037581,21.5191752838393));
#205273=CARTESIAN_POINT('Ctrl Pts',(-18.3101757995837,-16.8778587205445,
21.5147946921187));
#205274=CARTESIAN_POINT('Ctrl Pts',(-18.38160150593,-16.8632637924259,21.5104063595443));
#205275=CARTESIAN_POINT('Ctrl Pts',(-18.453691536507,-16.8523810078683,
21.5060180269699));
#205276=CARTESIAN_POINT('Ctrl Pts',(-18.5260293173379,-16.8452401192464,
21.5016296943955));
#205277=CARTESIAN_POINT('Ctrl Pts',(-18.5750331047421,-16.8404026666194,
21.4986569059845));
#205278=CARTESIAN_POINT('Ctrl Pts',(-18.6241504958208,-16.8372813242577,
21.4956841175734));
#205279=CARTESIAN_POINT('Ctrl Pts',(-18.6732524736177,-16.8358717576578,
21.4927113291624));
#205280=CARTESIAN_POINT('Ctrl Pts',(-18.7457477453063,-16.833790641617,
21.4883222370484));
#205281=CARTESIAN_POINT('Ctrl Pts',(-18.8184909189991,-16.8354351540471,
21.4839331449344));
#205282=CARTESIAN_POINT('Ctrl Pts',(-18.8910671368434,-16.8408347022263,
21.4795440528204));
#205283=CARTESIAN_POINT('Ctrl Pts',(-18.9635359887558,-16.8462262625614,
21.4751614537282));
#205284=CARTESIAN_POINT('Ctrl Pts',(-19.0358378982521,-16.8553617955042,
21.470778854636));
#205285=CARTESIAN_POINT('Ctrl Pts',(-19.107556633465,-16.8682187155092,
21.4663962555438));
#205286=CARTESIAN_POINT('Ctrl Pts',(-19.1791915242117,-16.8810606048308,
21.4620187800316));
#205287=CARTESIAN_POINT('Ctrl Pts',(-19.2502441227826,-16.8976151540491,
21.4576413045195));
#205288=CARTESIAN_POINT('Ctrl Pts',(-19.3203036537857,-16.9178080165438,
21.4532638290073));
#205289=CARTESIAN_POINT('Ctrl Pts',(-19.3903190046979,-16.9379881452606,
21.4488891139657));
#205290=CARTESIAN_POINT('Ctrl Pts',(-19.4593420684319,-16.9618019016887,
21.444514398924));
#205291=CARTESIAN_POINT('Ctrl Pts',(-19.5269739887336,-16.989124238982,
21.4401396838823));
#205292=CARTESIAN_POINT('Ctrl Pts',(-19.5945855447919,-17.0164383494096,
21.435766286085));
#205293=CARTESIAN_POINT('Ctrl Pts',(-19.6608063422521,-17.0472587627945,
21.4313928882876));
#205294=CARTESIAN_POINT('Ctrl Pts',(-19.7252559661585,-17.0814116942643,
21.4270194904902));
#205295=CARTESIAN_POINT('Ctrl Pts',(-19.7897074198449,-17.115565595365,
21.4226459685284));
#205296=CARTESIAN_POINT('Ctrl Pts',(-19.852387175046,-17.1530519748722,
21.4182724465665));
#205297=CARTESIAN_POINT('Ctrl Pts',(-19.9129394590442,-17.1936511290678,
21.4138989246046));
#205298=CARTESIAN_POINT('Ctrl Pts',(-19.9735547443612,-17.2342925244489,
21.4095208522338));
#205299=CARTESIAN_POINT('Ctrl Pts',(-20.0320377377389,-17.2780528916324,
21.4051427798631));
#205300=CARTESIAN_POINT('Ctrl Pts',(-20.0880624200393,-17.3246696823824,
21.4007647074923));
#205301=CARTESIAN_POINT('Ctrl Pts',(-20.1441178009626,-17.3713120167183,
21.3963842361647));
#205302=CARTESIAN_POINT('Ctrl Pts',(-20.1977118344489,-17.420813563513,
21.3920037648371));
#205303=CARTESIAN_POINT('Ctrl Pts',(-20.2485543554084,-17.4728738713303,
21.3876232935095));
#205304=CARTESIAN_POINT('Ctrl Pts',(-20.2994870055889,-17.5250264671557,
21.3832350568615));
#205305=CARTESIAN_POINT('Ctrl Pts',(-20.3476580839202,-17.5797465198983,
21.3788468202134));
#205306=CARTESIAN_POINT('Ctrl Pts',(-20.3928171932228,-17.6366998367413,
21.3744585835654));
#205307=CARTESIAN_POINT('Ctrl Pts',(-20.4234261084619,-17.6753028843823,
21.3714842298706));
#205308=CARTESIAN_POINT('Ctrl Pts',(-20.4526521461855,-17.7149312605343,
21.3685098761757));
#205309=CARTESIAN_POINT('Ctrl Pts',(-20.4804290453301,-17.7554739494572,
21.3655355224809));
#205310=CARTESIAN_POINT('Ctrl Pts',(-20.5219934386079,-17.8161406300021,
21.3610848022592));
#205311=CARTESIAN_POINT('Ctrl Pts',(-20.5604705880664,-17.8790885273535,
21.3566340820375));
#205312=CARTESIAN_POINT('Ctrl Pts',(-20.5956057988651,-17.943975769323,
21.3521833618158));
#205313=CARTESIAN_POINT('Ctrl Pts',(-20.6306759128556,-18.0087427913695,
21.3477408876718));
#205314=CARTESIAN_POINT('Ctrl Pts',(-20.6624161763064,-18.0754416108878,
21.3432984135279));
#205315=CARTESIAN_POINT('Ctrl Pts',(-20.6906149891654,-18.1437013026279,
21.3388559393839));
#205316=CARTESIAN_POINT('Ctrl Pts',(-20.701834052255,-18.1708588213483,
21.3370884749894));
#205317=CARTESIAN_POINT('Ctrl Pts',(-20.712493028082,-18.198263095923,21.3353210105949));
#205318=CARTESIAN_POINT('Ctrl Pts',(-20.7225805737622,-18.2258896078036,
21.3335535462005));
#205319=CARTESIAN_POINT('',(-17.1140743056113,-20.3149122292574,22.));
#205320=CARTESIAN_POINT('Origin',(-18.734,-18.952,22.));
#205321=CARTESIAN_POINT('Ctrl Pts',(-20.7225805737622,-18.2258896078036,
21.5555703780636));
#205322=CARTESIAN_POINT('Ctrl Pts',(-20.6978890798413,-18.1582676240448,
21.5598847419305));
#205323=CARTESIAN_POINT('Ctrl Pts',(-20.669739897526,-18.0918946295011,
21.5641991057974));
#205324=CARTESIAN_POINT('Ctrl Pts',(-20.6382937604498,-18.0271463500035,
21.5685134696643));
#205325=CARTESIAN_POINT('Ctrl Pts',(-20.606820934294,-17.962343117111,21.5728314952338));
#205326=CARTESIAN_POINT('Ctrl Pts',(-20.5720457802183,-17.8991678020743,
21.5771495208033));
#205327=CARTESIAN_POINT('Ctrl Pts',(-20.5341758304195,-17.8379730795113,
21.5814675463728));
#205328=CARTESIAN_POINT('Ctrl Pts',(-20.4962904117645,-17.7767533605497,
21.5857873357396));
#205329=CARTESIAN_POINT('Ctrl Pts',(-20.4553079633058,-17.7175162539135,
21.5901071251064));
#205330=CARTESIAN_POINT('Ctrl Pts',(-20.4114787620569,-17.6605844964351,
21.5944269144732));
#205331=CARTESIAN_POINT('Ctrl Pts',(-20.3675727878446,-17.6035530150371,
21.598754270554));
#205332=CARTESIAN_POINT('Ctrl Pts',(-20.3208104248372,-17.5488353262228,
21.6030816266348));
#205333=CARTESIAN_POINT('Ctrl Pts',(-20.2714810943291,-17.4967196543001,
21.6074089827156));
#205334=CARTESIAN_POINT('Ctrl Pts',(-20.2294415799254,-17.4523055599289,
21.6110968484623));
#205335=CARTESIAN_POINT('Ctrl Pts',(-20.1855384940817,-17.4097807538747,
21.614784714209));
#205336=CARTESIAN_POINT('Ctrl Pts',(-20.1399695509607,-17.369300211104,
21.6184725799558));
#205337=CARTESIAN_POINT('Ctrl Pts',(-20.0856805133166,-17.3210732925096,
21.6228661574372));
#205338=CARTESIAN_POINT('Ctrl Pts',(-20.0288041823845,-17.2755513561322,
21.6272597349186));
#205339=CARTESIAN_POINT('Ctrl Pts',(-19.969640873017,-17.2330233762701,
21.6316533124001));
#205340=CARTESIAN_POINT('Ctrl Pts',(-19.9105638618643,-17.1905574295968,
21.6360404812154));
#205341=CARTESIAN_POINT('Ctrl Pts',(-19.849206882515,-17.1510770477242,
21.6404276500308));
#205342=CARTESIAN_POINT('Ctrl Pts',(-19.7859046048043,-17.1148321518186,
21.6448148188462));
#205343=CARTESIAN_POINT('Ctrl Pts',(-19.7226747936877,-17.0786287480086,
21.6491969653592));
#205344=CARTESIAN_POINT('Ctrl Pts',(-19.6575045236034,-17.0456537097674,
21.6535791118721));
#205345=CARTESIAN_POINT('Ctrl Pts',(-19.5907574447862,-17.0161137221408,
21.6579612583851));
#205346=CARTESIAN_POINT('Ctrl Pts',(-19.524051506928,-16.9865919421039,
21.6623407038703));
#205347=CARTESIAN_POINT('Ctrl Pts',(-19.4557711276412,-16.960501205489,
21.6667201493556));
#205348=CARTESIAN_POINT('Ctrl Pts',(-19.3863033026644,-16.9380016382,21.6710995948408));
#205349=CARTESIAN_POINT('Ctrl Pts',(-19.3168555527303,-16.9155085729106,
21.6754777747394));
#205350=CARTESIAN_POINT('Ctrl Pts',(-19.2462214956912,-16.8966047644762,
21.6798559546379));
#205351=CARTESIAN_POINT('Ctrl Pts',(-19.1748052243022,-16.8814011121833,
21.6842341345365));
#205352=CARTESIAN_POINT('Ctrl Pts',(-19.10338621101,-16.8661968761726,21.6886124825276));
#205353=CARTESIAN_POINT('Ctrl Pts',(-19.0311853945028,-16.8546931765608,
21.6929908305188));
#205354=CARTESIAN_POINT('Ctrl Pts',(-18.958617414822,-16.8469498778037,
21.6973691785099));
#205355=CARTESIAN_POINT('Ctrl Pts',(-18.8859734847581,-16.8391984748317,
21.7017521089244));
#205356=CARTESIAN_POINT('Ctrl Pts',(-18.8129621034892,-16.835215381558,
21.7061350393389));
#205357=CARTESIAN_POINT('Ctrl Pts',(-18.7400025813939,-16.8350085099329,
21.7105179697534));
#205358=CARTESIAN_POINT('Ctrl Pts',(-18.6670027054265,-16.8348015238872,
21.7149033243644));
#205359=CARTESIAN_POINT('Ctrl Pts',(-18.5940552263849,-16.8383748946447,
21.7192886789753));
#205360=CARTESIAN_POINT('Ctrl Pts',(-18.5215762918332,-16.8456844566379,
21.7236740335863));
#205361=CARTESIAN_POINT('Ctrl Pts',(-18.4489692699444,-16.8530069363477,
21.728067138151));
#205362=CARTESIAN_POINT('Ctrl Pts',(-18.3768329218414,-16.8640787198162,
21.7324602427158));
#205363=CARTESIAN_POINT('Ctrl Pts',(-18.3055745682925,-16.8788042423673,
21.7368533472805));
#205364=CARTESIAN_POINT('Ctrl Pts',(-18.2580212556926,-16.8886311235987,
21.739785027066));
#205365=CARTESIAN_POINT('Ctrl Pts',(-18.2108587080193,-16.900084095337,
21.7427167068516));
#205366=CARTESIAN_POINT('Ctrl Pts',(-18.1642037039559,-16.913122568418,
21.7456483866372));
#205367=CARTESIAN_POINT('Ctrl Pts',(-18.0951065059757,-16.932432864793,
21.7499902758433));
#205368=CARTESIAN_POINT('Ctrl Pts',(-18.0268409185985,-16.9553020920462,
21.7543321650495));
#205369=CARTESIAN_POINT('Ctrl Pts',(-17.9598056269363,-16.9816416385042,
21.7586740542557));
#205370=CARTESIAN_POINT('Ctrl Pts',(-17.8928712802768,-17.007941521592,
21.7630094052339));
#205371=CARTESIAN_POINT('Ctrl Pts',(-17.8271640088704,-17.0377011783514,
21.7673447562122));
#205372=CARTESIAN_POINT('Ctrl Pts',(-17.7630690182321,-17.0707817700641,
21.7716801071904));
#205373=CARTESIAN_POINT('Ctrl Pts',(-17.6990476945068,-17.1038243409416,
21.7760104753779));
#205374=CARTESIAN_POINT('Ctrl Pts',(-17.6366354094004,-17.140180045608,
21.7803408435655));
#205375=CARTESIAN_POINT('Ctrl Pts',(-17.576197298269,-17.1796620232404,
21.784671211753));
#205376=CARTESIAN_POINT('Ctrl Pts',(-17.5157963311547,-17.2191197360633,
21.7889989185855));
#205377=CARTESIAN_POINT('Ctrl Pts',(-17.4573675446825,-17.2616996436244,
21.793326625418));
#205378=CARTESIAN_POINT('Ctrl Pts',(-17.4012499559382,-17.3071698202996,
21.7976543322506));
#205379=CARTESIAN_POINT('Ctrl Pts',(-17.3451474140536,-17.3526278050152,
21.8019808786911));
#205380=CARTESIAN_POINT('Ctrl Pts',(-17.2913552237362,-17.4009742110386,
21.8063074251317));
#205381=CARTESIAN_POINT('Ctrl Pts',(-17.2401804886106,-17.4519359122383,
21.8106339715723));
#205382=CARTESIAN_POINT('Ctrl Pts',(-17.1890017454992,-17.502901604739,
21.8149608568663));
#205383=CARTESIAN_POINT('Ctrl Pts',(-17.1404412125279,-17.5564826492106,
21.8192877421603));
#205384=CARTESIAN_POINT('Ctrl Pts',(-17.0947688687351,-17.6123693425829,
21.8236146274544));
#205385=CARTESIAN_POINT('Ctrl Pts',(-17.0490417134499,-17.6683231057134,
21.8279467054541));
#205386=CARTESIAN_POINT('Ctrl Pts',(-17.0062099790967,-17.7265876580954,
21.8322787834538));
#205387=CARTESIAN_POINT('Ctrl Pts',(-16.9665025074284,-17.7868212095334,
21.8366108614535));
#205388=CARTESIAN_POINT('Ctrl Pts',(-16.9267705288898,-17.8470919362378,
21.8409456131484));
#205389=CARTESIAN_POINT('Ctrl Pts',(-16.8901668972173,-17.9093336530359,
21.8452803648433));
#205390=CARTESIAN_POINT('Ctrl Pts',(-16.8568748225048,-17.9731792462286,
21.8496151165381));
#205391=CARTESIAN_POINT('Ctrl Pts',(-16.8235156981184,-18.0371534233633,
21.8539585983494));
#205392=CARTESIAN_POINT('Ctrl Pts',(-16.7934816509746,-18.1027374769631,
21.8583020801606));
#205393=CARTESIAN_POINT('Ctrl Pts',(-16.7669077870852,-18.1695441061056,
21.8626455619719));
#205394=CARTESIAN_POINT('Ctrl Pts',(-16.7461498194961,-18.221729586104,
21.8660384390875));
#205395=CARTESIAN_POINT('Ctrl Pts',(-16.7275022238381,-18.2746606281223,
21.869431316203));
#205396=CARTESIAN_POINT('Ctrl Pts',(-16.7110077838934,-18.328147859207,
21.8728241933186));
#205397=CARTESIAN_POINT('Ctrl Pts',(-16.6890805388882,-18.3992522813377,
21.8773345888236));
#205398=CARTESIAN_POINT('Ctrl Pts',(-16.6708712302021,-18.471627433023,
21.8818449843287));
#205399=CARTESIAN_POINT('Ctrl Pts',(-16.65651913225,-18.5448609032129,21.8863553798337));
#205400=CARTESIAN_POINT('Ctrl Pts',(-16.6414517292682,-18.6217443115328,
21.8910905723407));
#205401=CARTESIAN_POINT('Ctrl Pts',(-16.6306362647773,-18.699573380232,
21.8958257648476));
#205402=CARTESIAN_POINT('Ctrl Pts',(-16.6241750600365,-18.7778514349529,
21.9005609573545));
#205403=CARTESIAN_POINT('Ctrl Pts',(-16.6180410539461,-18.8521654497015,
21.9050563573367));
#205404=CARTESIAN_POINT('Ctrl Pts',(-16.6158311159158,-18.9268835670766,
21.9095517573189));
#205405=CARTESIAN_POINT('Ctrl Pts',(-16.6175804464527,-19.001570892293,
21.9140471573011));
#205406=CARTESIAN_POINT('Ctrl Pts',(-16.6193281321099,-19.0761879896894,
21.9185383302991));
#205407=CARTESIAN_POINT('Ctrl Pts',(-16.6250276759246,-19.1507739043837,
21.9230295032971));
#205408=CARTESIAN_POINT('Ctrl Pts',(-16.6346622676094,-19.2248920763987,
21.9275206762951));
#205409=CARTESIAN_POINT('Ctrl Pts',(-16.6442903170874,-19.2989599197204,
21.932008799638));
#205410=CARTESIAN_POINT('Ctrl Pts',(-16.6578480436051,-19.3725602066461,
21.9364969229808));
#205411=CARTESIAN_POINT('Ctrl Pts',(-16.6752667781491,-19.4452611085899,
21.9409850463236));
#205412=CARTESIAN_POINT('Ctrl Pts',(-16.6926782312815,-19.5179316199686,
21.9454712935328));
#205413=CARTESIAN_POINT('Ctrl Pts',(-16.7139473766674,-19.5897030572418,
21.949957540742));
#205414=CARTESIAN_POINT('Ctrl Pts',(-16.7389546395216,-19.6601546509298,
21.9544437879513));
#205415=CARTESIAN_POINT('Ctrl Pts',(-16.7639650091895,-19.7306149972742,
21.9589305925159));
#205416=CARTESIAN_POINT('Ctrl Pts',(-16.792714280612,-19.7997547457854,
21.9634173970806));
#205417=CARTESIAN_POINT('Ctrl Pts',(-16.8250335623977,-19.8671700061235,
21.9679042016453));
#205418=CARTESIAN_POINT('Ctrl Pts',(-16.8573543979593,-19.9345885075052,
21.9723912219168));
#205419=CARTESIAN_POINT('Ctrl Pts',(-16.8932453841005,-20.0002819530908,
21.9768782421882));
#205420=CARTESIAN_POINT('Ctrl Pts',(-16.9324909433493,-20.0638696500964,
21.9813652624597));
#205421=CARTESIAN_POINT('Ctrl Pts',(-16.971763585854,-20.1275012288023,
21.9858553792119));
#205422=CARTESIAN_POINT('Ctrl Pts',(-17.0143951804746,-20.1890237784353,
21.9903454959641));
#205423=CARTESIAN_POINT('Ctrl Pts',(-17.0601263939598,-20.2480849320172,
21.9948356127163));
#205424=CARTESIAN_POINT('Ctrl Pts',(-17.0776592489258,-20.2707283425231,
21.9965570751442));
#205425=CARTESIAN_POINT('Ctrl Pts',(-17.0956472766607,-20.2930102923405,
21.9982785375721));
#205426=CARTESIAN_POINT('Ctrl Pts',(-17.1140743056112,-20.3149122292573,
22.));
#205427=CARTESIAN_POINT('Origin',(-23.734,10.1295,7.));
#205428=CARTESIAN_POINT('',(-17.7339261105301,14.3917184061412,6.91639119908484));
#205429=CARTESIAN_POINT('Ctrl Pts',(-17.7339050342228,14.3916804139849,
6.91641101362463));
#205430=CARTESIAN_POINT('Ctrl Pts',(-17.747271947537,14.3963166964844,7.15281383796445));
#205431=CARTESIAN_POINT('Ctrl Pts',(-17.7606435542079,14.381276775214,7.3891987374152));
#205432=CARTESIAN_POINT('Ctrl Pts',(-17.7868173786296,14.3129820114568,
7.85141300883512));
#205433=CARTESIAN_POINT('Ctrl Pts',(-17.7995847185911,14.2607676448875,
8.0765946212184));
#205434=CARTESIAN_POINT('Ctrl Pts',(-17.8351210560246,14.0658910059837,
8.68704183225604));
#205435=CARTESIAN_POINT('Ctrl Pts',(-17.8583311393401,13.8854986826804,
9.05760511570486));
#205436=CARTESIAN_POINT('Ctrl Pts',(-17.896785360625,13.501055669657,9.62312009133906));
#205437=CARTESIAN_POINT('Ctrl Pts',(-17.9119488674433,13.3256514205499,
9.83421379898093));
#205438=CARTESIAN_POINT('Ctrl Pts',(-17.9585784805536,12.7284406416945,
10.4264305443397));
#205439=CARTESIAN_POINT('Ctrl Pts',(-17.9907455843245,12.249980031746,10.7414542056046));
#205440=CARTESIAN_POINT('Ctrl Pts',(-18.0356184383294,11.5020306423617,
11.0430893364069));
#205441=CARTESIAN_POINT('Ctrl Pts',(-18.0487838384663,11.2730044491194,
11.1137338665646));
#205442=CARTESIAN_POINT('Ctrl Pts',(-18.0792554367816,10.7400986580418,
11.2301431695451));
#205443=CARTESIAN_POINT('Ctrl Pts',(-18.0966642257857,10.4350814532254,
11.2629999729017));
#205444=CARTESIAN_POINT('Ctrl Pts',(-18.1138504934428,10.1295003780333,
11.263));
#205445=CARTESIAN_POINT('Origin',(-17.734,10.1295,7.));
#205446=CARTESIAN_POINT('Origin',(23.734,10.1295,7.));
#205447=CARTESIAN_POINT('',(23.5339999818689,7.33961491412,10.2235360410646));
#205448=CARTESIAN_POINT('Ctrl Pts',(23.533999981869,7.33961491412,10.2235360410646));
#205449=CARTESIAN_POINT('Ctrl Pts',(23.5009788547464,6.89416391178422,9.83730563779939));
#205450=CARTESIAN_POINT('Ctrl Pts',(23.4291758459878,6.10016038128925,8.79502345374907));
#205451=CARTESIAN_POINT('Ctrl Pts',(23.3185909555934,5.6985094017683,6.80076298606476));
#205452=CARTESIAN_POINT('Ctrl Pts',(23.2022453106851,6.3076790998453,4.74899581907506));
#205453=CARTESIAN_POINT('Ctrl Pts',(23.085899665777,7.80672899094502,3.22136567669558));
#205454=CARTESIAN_POINT('Ctrl Pts',(22.9695540208687,9.84662493401956,2.57356512891912));
#205455=CARTESIAN_POINT('Ctrl Pts',(22.8532083759605,11.9523856169729,2.95643327596383));
#205456=CARTESIAN_POINT('Ctrl Pts',(22.7368627310523,13.6336979697146,4.28082124831138));
#205457=CARTESIAN_POINT('Ctrl Pts',(22.6205170861441,14.4990821903827,6.2383517396752));
#205458=CARTESIAN_POINT('Ctrl Pts',(22.5041714412359,14.3470299002299,8.3732307562808));
#205459=CARTESIAN_POINT('Ctrl Pts',(22.3878257963277,13.2129653049274,10.1883541012585));
#205460=CARTESIAN_POINT('Ctrl Pts',(22.2878747590527,11.6218855899156,11.109940009747));
#205461=CARTESIAN_POINT('Ctrl Pts',(22.2267056034138,10.5292997601409,11.262549287517));
#205462=CARTESIAN_POINT('Ctrl Pts',(22.2043183294109,10.1294634667828,11.26269919276));
#205463=CARTESIAN_POINT('',(23.534,7.33966741897454,3.77664721604215));
#205464=CARTESIAN_POINT('Origin',(23.534,10.1295,7.));
#205465=CARTESIAN_POINT('Ctrl Pts',(23.534,7.33966741897454,3.77664721604215));
#205466=CARTESIAN_POINT('Ctrl Pts',(23.5171384228933,7.56733156584535,3.57960243160758));
#205467=CARTESIAN_POINT('Ctrl Pts',(23.5006043298958,7.81523356358243,3.40722905341181));
#205468=CARTESIAN_POINT('Ctrl Pts',(23.4677316209677,8.33075529092307,3.12443663545715));
#205469=CARTESIAN_POINT('Ctrl Pts',(23.4515038045768,8.5955661823329,3.0122045914911));
#205470=CARTESIAN_POINT('Ctrl Pts',(23.41251419603,9.25346884470398,2.80867864495278));
#205471=CARTESIAN_POINT('Ctrl Pts',(23.3905041575587,9.65217768291865,2.74479412039573));
#205472=CARTESIAN_POINT('Ctrl Pts',(23.3528764260495,10.3266429480868,2.73283385968559));
#205473=CARTESIAN_POINT('Ctrl Pts',(23.3374995684002,10.5991983511286,2.75418468589991));
#205474=CARTESIAN_POINT('Ctrl Pts',(23.28999893921,11.4262024328021,2.89961566339959));
#205475=CARTESIAN_POINT('Ctrl Pts',(23.2592781393447,11.9594174069227,3.10821363505845));
#205476=CARTESIAN_POINT('Ctrl Pts',(23.2141339367492,12.6330052456083,3.54161899737083));
#205477=CARTESIAN_POINT('Ctrl Pts',(23.2008471051019,12.8190500942101,3.68424101884531));
#205478=CARTESIAN_POINT('Ctrl Pts',(23.16494641965,13.2927988981491,4.11364698227542));
#205479=CARTESIAN_POINT('Ctrl Pts',(23.142856411777,13.5527887079619,4.4273370726122));
#205480=CARTESIAN_POINT('Ctrl Pts',(23.1071703914128,13.8847096290569,4.96912126006405));
#205481=CARTESIAN_POINT('Ctrl Pts',(23.0941377991731,13.9887911184171,5.17464059795072));
#205482=CARTESIAN_POINT('Ctrl Pts',(23.0660637765397,14.1768533050884,5.63489940988804));
#205483=CARTESIAN_POINT('Ctrl Pts',(23.0512908040241,14.2544426432218,5.89120750097675));
#205484=CARTESIAN_POINT('Ctrl Pts',(23.0104953092479,14.4005588632585,6.61204200382184));
#205485=CARTESIAN_POINT('Ctrl Pts',(22.9840977251256,14.4173311561388,7.0831920722925));
#205486=CARTESIAN_POINT('Ctrl Pts',(22.9428531767094,14.3231670213471,7.81023920356386));
#205487=CARTESIAN_POINT('Ctrl Pts',(22.928285381263,14.2647372016801,8.06918027130044));
#205488=CARTESIAN_POINT('Ctrl Pts',(22.8916271555053,14.0602543447828,8.69657156102269));
#205489=CARTESIAN_POINT('Ctrl Pts',(22.8693565843284,13.886253987401,9.05328041975969));
#205490=CARTESIAN_POINT('Ctrl Pts',(22.8320314201182,13.5168336638794,9.60195233611007));
#205491=CARTESIAN_POINT('Ctrl Pts',(22.8173170927165,13.3476009303476,9.80856107552979));
#205492=CARTESIAN_POINT('Ctrl Pts',(22.776903461955,12.8353140666472,10.3264293462766));
#205493=CARTESIAN_POINT('Ctrl Pts',(22.7508427647092,12.4592147251802,10.5998547238669));
#205494=CARTESIAN_POINT('Ctrl Pts',(22.6994960602955,11.643957736814,11.0103447464061));
#205495=CARTESIAN_POINT('Ctrl Pts',(22.6749861462296,11.2116364346642,11.1479431088793));
#205496=CARTESIAN_POINT('Ctrl Pts',(22.6376197358264,10.555150792154,11.2470440165433));
#205497=CARTESIAN_POINT('Ctrl Pts',(22.6255433575552,10.3424480415559,11.2630000045993));
#205498=CARTESIAN_POINT('Ctrl Pts',(22.6135314140065,10.129499907926,11.263));
#205499=CARTESIAN_POINT('Origin',(-18.734,-18.952,-1.76670989022851));
#205500=CARTESIAN_POINT('',(-21.2939992553327,-18.9539526125931,21.7667098902285));
#205501=CARTESIAN_POINT('Ctrl Pts',(-17.1722616776481,-20.9849677398537,
21.4832513321535));
#205502=CARTESIAN_POINT('Ctrl Pts',(-17.2221126184485,-21.0237381697153,
21.4864046644898));
#205503=CARTESIAN_POINT('Ctrl Pts',(-17.963685564347,-21.5551355225752,
21.5319499323866));
#205504=CARTESIAN_POINT('Ctrl Pts',(-19.9618261650098,-21.7191790573139,
21.6198871358439));
#205505=CARTESIAN_POINT('Ctrl Pts',(-21.2281784624135,-20.0656258695291,
21.7112199895325));
#205506=CARTESIAN_POINT('Ctrl Pts',(-21.297142385429,-19.0852910214283,
21.7601609076607));
#205507=CARTESIAN_POINT('Ctrl Pts',(-21.2960080465361,-18.9539541447775,
21.7667098902285));
#205508=CARTESIAN_POINT('',(-18.072232390111,-16.4790132166747,21.9999999999826));
#205509=CARTESIAN_POINT('Ctrl Pts',(-21.2939992553327,-18.9539526125931,
21.7667098902285));
#205510=CARTESIAN_POINT('Ctrl Pts',(-21.2940622837578,-18.8713183400037,
21.7708336287807));
#205511=CARTESIAN_POINT('Ctrl Pts',(-21.290120073806,-18.7885361132696,
21.7749573673329));
#205512=CARTESIAN_POINT('Ctrl Pts',(-21.2821561914378,-18.7060324736127,
21.7790811058851));
#205513=CARTESIAN_POINT('Ctrl Pts',(-21.2742021133718,-18.6236304038401,
21.7831997677201));
#205514=CARTESIAN_POINT('Ctrl Pts',(-21.2622362429578,-18.5415067083406,
21.7873184295551));
#205515=CARTESIAN_POINT('Ctrl Pts',(-21.2462941819498,-18.4600874637281,
21.7914370913901));
#205516=CARTESIAN_POINT('Ctrl Pts',(-21.2303628128015,-18.3787228245485,
21.7955529909627));
#205517=CARTESIAN_POINT('Ctrl Pts',(-21.2104606337788,-18.2980621623454,
21.7996688905354));
#205518=CARTESIAN_POINT('Ctrl Pts',(-21.1866748711293,-18.2185247267081,
21.803784790108));
#205519=CARTESIAN_POINT('Ctrl Pts',(-21.1628974701717,-18.1390152518109,
21.8078992427696));
#205520=CARTESIAN_POINT('Ctrl Pts',(-21.1352393308965,-18.0606286731435,
21.8120136954312));
#205521=CARTESIAN_POINT('Ctrl Pts',(-21.1038380346635,-17.9837708486818,
21.8161281480927));
#205522=CARTESIAN_POINT('Ctrl Pts',(-21.0724377570491,-17.9069155173914,
21.8202424672866));
#205523=CARTESIAN_POINT('Ctrl Pts',(-21.0372947445442,-17.8315892795539,
21.8243567864805));
#205524=CARTESIAN_POINT('Ctrl Pts',(-20.9985948099081,-17.758178259983,
21.8284711056744));
#205525=CARTESIAN_POINT('Ctrl Pts',(-20.959859225451,-17.6846996152406,
21.8325892149197));
#205526=CARTESIAN_POINT('Ctrl Pts',(-20.9175603979486,-17.613140131245,
21.836707324165));
#205527=CARTESIAN_POINT('Ctrl Pts',(-20.8719298849008,-17.5438608707773,
21.8408254334103));
#205528=CARTESIAN_POINT('Ctrl Pts',(-20.8262774812034,-17.4745483744787,
21.8449455182654));
#205529=CARTESIAN_POINT('Ctrl Pts',(-20.7772904911253,-17.4075186609022,
21.8490656031205));
#205530=CARTESIAN_POINT('Ctrl Pts',(-20.7252420557879,-17.3431012849587,
21.8531856879756));
#205531=CARTESIAN_POINT('Ctrl Pts',(-20.6731075913472,-17.2785774357072,
21.85731258278));
#205532=CARTESIAN_POINT('Ctrl Pts',(-20.6179018945763,-17.2166748979188,
21.8614394775843));
#205533=CARTESIAN_POINT('Ctrl Pts',(-20.5599360513378,-17.1576874473981,
21.8655663723887));
#205534=CARTESIAN_POINT('Ctrl Pts',(-20.5193323481527,-17.1163681324571,
21.8684571646614));
#205535=CARTESIAN_POINT('Ctrl Pts',(-20.4773751065851,-17.076478372295,
21.871347956934));
#205536=CARTESIAN_POINT('Ctrl Pts',(-20.4341804678598,-17.0381070101209,
21.8742387492067));
#205537=CARTESIAN_POINT('Ctrl Pts',(-20.3717052812394,-16.9826080388726,
21.8784198881639));
#205538=CARTESIAN_POINT('Ctrl Pts',(-20.3063943198782,-16.9300688092441,
21.8826010271211));
#205539=CARTESIAN_POINT('Ctrl Pts',(-20.2385599097816,-16.8807927486903,
21.8867821660783));
#205540=CARTESIAN_POINT('Ctrl Pts',(-20.1708205215985,-16.8315857136584,
21.8909574481286));
#205541=CARTESIAN_POINT('Ctrl Pts',(-20.1005650755227,-16.7856330369313,
21.8951327301788));
#205542=CARTESIAN_POINT('Ctrl Pts',(-20.0281405702344,-16.7431993787412,
21.8993080122291));
#205543=CARTESIAN_POINT('Ctrl Pts',(-19.9553653729372,-16.7005602494225,
21.9035035117188));
#205544=CARTESIAN_POINT('Ctrl Pts',(-19.880400404287,-16.6614746253178,
21.9076990112086));
#205545=CARTESIAN_POINT('Ctrl Pts',(-19.8036290904368,-16.6261681898961,
21.9118945106983));
#205546=CARTESIAN_POINT('Ctrl Pts',(-19.7273611982937,-16.5910932735809,
21.916062498538));
#205547=CARTESIAN_POINT('Ctrl Pts',(-19.6493110036014,-16.5597483260403,
21.9202304863778));
#205548=CARTESIAN_POINT('Ctrl Pts',(-19.5698794212801,-16.5323087814598,
21.9243984742175));
#205549=CARTESIAN_POINT('Ctrl Pts',(-19.4904728949047,-16.5048778924257,
21.9285651473047));
#205550=CARTESIAN_POINT('Ctrl Pts',(-19.4096862815083,-16.4813501100524,
21.9327318203918));
#205551=CARTESIAN_POINT('Ctrl Pts',(-19.3279387681294,-16.4618520646932,
21.936898493479));
#205552=CARTESIAN_POINT('Ctrl Pts',(-19.2461924230011,-16.4423542979797,
21.9410651070204));
#205553=CARTESIAN_POINT('Ctrl Pts',(-19.1634856536714,-16.4268862595724,
21.9452317205618));
#205554=CARTESIAN_POINT('Ctrl Pts',(-19.0802496942046,-16.415523871734,
21.9493983341032));
#205555=CARTESIAN_POINT('Ctrl Pts',(-18.9960110559548,-16.4040246100579,
21.9536151395932));
#205556=CARTESIAN_POINT('Ctrl Pts',(-18.9112308686983,-16.39673065975,21.9578319450831));
#205557=CARTESIAN_POINT('Ctrl Pts',(-18.8263615920593,-16.3936666878,21.962048750573));
#205558=CARTESIAN_POINT('Ctrl Pts',(-18.742380245673,-16.3906347721311,
21.9662214384587));
#205559=CARTESIAN_POINT('Ctrl Pts',(-18.6583121305892,-16.3917446684187,
21.9703941263443));
#205560=CARTESIAN_POINT('Ctrl Pts',(-18.5745939384244,-16.3969677678094,
21.97456681423));
#205561=CARTESIAN_POINT('Ctrl Pts',(-18.4895480243537,-16.402273702523,
21.9788056785221));
#205562=CARTESIAN_POINT('Ctrl Pts',(-18.4048637212048,-16.4118243850528,
21.9830445428142));
#205563=CARTESIAN_POINT('Ctrl Pts',(-18.3209897195339,-16.4255355715488,
21.9872834071063));
#205564=CARTESIAN_POINT('Ctrl Pts',(-18.237115717863,-16.4392467580448,
21.9915222713984));
#205565=CARTESIAN_POINT('Ctrl Pts',(-18.1540524839651,-16.4571182804316,
21.9957611356905));
#205566=CARTESIAN_POINT('Ctrl Pts',(-18.072232390111,-16.4790132166747,
21.9999999999825));
#205567=CARTESIAN_POINT('',(-19.3957372685685,-16.4790050975816,22.));
#205568=CARTESIAN_POINT('Origin',(-18.734,-18.952,22.));
#205569=CARTESIAN_POINT('',(-21.2914666104891,-18.9488558930302,21.8332901097715));
#205570=CARTESIAN_POINT('Ctrl Pts',(-21.2914666104891,-18.9488558930302,
21.8332901097715));
#205571=CARTESIAN_POINT('Ctrl Pts',(-21.2935045175504,-18.6834066038016,
21.8464681376205));
#205572=CARTESIAN_POINT('Ctrl Pts',(-21.1334434961762,-17.5672072134799,
21.90203810103));
#205573=CARTESIAN_POINT('Ctrl Pts',(-20.2191097516036,-16.6993275322964,
21.9576080644395));
#205574=CARTESIAN_POINT('Ctrl Pts',(-19.3957372685685,-16.4790050975816,
22.));
#205575=CARTESIAN_POINT('Ctrl Pts',(-17.176996236551,-20.9788220778502,
21.5499224931685));
#205576=CARTESIAN_POINT('Ctrl Pts',(-17.5432452950599,-21.2588471679196,
21.5727725220976));
#205577=CARTESIAN_POINT('Ctrl Pts',(-18.7954429833719,-21.7916144582144,
21.6380144865871));
#205578=CARTESIAN_POINT('Ctrl Pts',(-20.7940987275605,-20.9887402433146,
21.7324703587881));
#205579=CARTESIAN_POINT('Ctrl Pts',(-21.2869488458059,-19.5373211115314,
21.80407620206));
#205580=CARTESIAN_POINT('Ctrl Pts',(-21.2914666104891,-18.9488558930302,
21.8332901097715));
#205581=CARTESIAN_POINT('Origin',(18.734,-18.952,-1.76670989022851));
#205582=CARTESIAN_POINT('',(16.1740007447319,-18.9539526972956,21.7667098902285));
#205583=CARTESIAN_POINT('Ctrl Pts',(20.2957383325669,-20.9849679853861,
21.4832513385096));
#205584=CARTESIAN_POINT('Ctrl Pts',(20.245887419744,-21.0237383877019,21.4864046687272));
#205585=CARTESIAN_POINT('Ctrl Pts',(19.5043144385534,-21.5551357017593,
21.5319499345053));
#205586=CARTESIAN_POINT('Ctrl Pts',(17.5061736134544,-21.7191789276414,
21.6198871358439));
#205587=CARTESIAN_POINT('Ctrl Pts',(16.2398215663958,-20.0656261776283,
21.7112199895325));
#205588=CARTESIAN_POINT('Ctrl Pts',(16.1708575232621,-19.0852911366623,
21.7601609076608));
#205589=CARTESIAN_POINT('Ctrl Pts',(16.1719918438157,-18.9539542296302,
21.7667098902285));
#205590=CARTESIAN_POINT('',(19.3957679668415,-16.4790133121946,21.9999999999819));
#205591=CARTESIAN_POINT('Ctrl Pts',(16.1740007447319,-18.9539526972956,
21.7667098902285));
#205592=CARTESIAN_POINT('Ctrl Pts',(16.1739377135638,-18.8713184130896,
21.770833628584));
#205593=CARTESIAN_POINT('Ctrl Pts',(16.1778799218946,-18.788536175973,21.7749573669396));
#205594=CARTESIAN_POINT('Ctrl Pts',(16.1858438033836,-18.7060325272615,
21.7790811052951));
#205595=CARTESIAN_POINT('Ctrl Pts',(16.1937978807278,-18.6236304468261,
21.7831997670146));
#205596=CARTESIAN_POINT('Ctrl Pts',(16.2057637513171,-18.5415067419994,
21.787318428734));
#205597=CARTESIAN_POINT('Ctrl Pts',(16.2217058130157,-18.4600874894405,
21.7914370904535));
#205598=CARTESIAN_POINT('Ctrl Pts',(16.2376371830466,-18.3787228413373,
21.7955529899605));
#205599=CARTESIAN_POINT('Ctrl Pts',(16.2575393635618,-18.2980621716067,
21.7996688894674));
#205600=CARTESIAN_POINT('Ctrl Pts',(16.2813251279379,-18.2185247298273,
21.8037847889744));
#205601=CARTESIAN_POINT('Ctrl Pts',(16.3051025309066,-18.1390152478367,
21.8078992416196));
#205602=CARTESIAN_POINT('Ctrl Pts',(16.3327606725192,-18.0606286634871,
21.8120136942648));
#205603=CARTESIAN_POINT('Ctrl Pts',(16.3641619710533,-17.9837708346894,
21.81612814691));
#205604=CARTESIAN_POINT('Ctrl Pts',(16.3955622513427,-17.9069154981479,
21.8202424661365));
#205605=CARTESIAN_POINT('Ctrl Pts',(16.4307052665747,-17.8315892564417,
21.824356785363));
#205606=CARTESIAN_POINT('Ctrl Pts',(16.4694052036476,-17.7581782342687,
21.8284711045895));
#205607=CARTESIAN_POINT('Ctrl Pts',(16.5081407912399,-17.6846995856018,
21.8325892139415));
#205608=CARTESIAN_POINT('Ctrl Pts',(16.5504396217143,-17.6131400990192,
21.8367073232935));
#205609=CARTESIAN_POINT('Ctrl Pts',(16.5960701372503,-17.543860837146,21.8408254326455));
#205610=CARTESIAN_POINT('Ctrl Pts',(16.6417225438979,-17.4745483387419,
21.8449455176489));
#205611=CARTESIAN_POINT('Ctrl Pts',(16.6907095365087,-17.407518624288,21.8490656026523));
#205612=CARTESIAN_POINT('Ctrl Pts',(16.7427579736743,-17.3431012484951,
21.8531856876557));
#205613=CARTESIAN_POINT('Ctrl Pts',(16.794892440757,-17.2785773983907,21.8573125826728));
#205614=CARTESIAN_POINT('Ctrl Pts',(16.850098139558,-17.2166748608617,21.8614394776899));
#205615=CARTESIAN_POINT('Ctrl Pts',(16.9080639839603,-17.1576874114779,
21.865566372707));
#205616=CARTESIAN_POINT('Ctrl Pts',(16.9486676843771,-17.1163681009799,
21.8684571648736));
#205617=CARTESIAN_POINT('Ctrl Pts',(16.9906249225133,-17.0764783454379,
21.8713479570401));
#205618=CARTESIAN_POINT('Ctrl Pts',(17.0338195571032,-17.0381069879455,
21.8742387492067));
#205619=CARTESIAN_POINT('Ctrl Pts',(17.0962945700832,-16.9826081724059,
21.8784198767899));
#205620=CARTESIAN_POINT('Ctrl Pts',(17.1616053466634,-16.9300690778322,
21.8826010043731));
#205621=CARTESIAN_POINT('Ctrl Pts',(17.2294395634032,-16.8807931313779,
21.8867821319562));
#205622=CARTESIAN_POINT('Ctrl Pts',(17.2971787572344,-16.8315862112052,
21.8909574025704));
#205623=CARTESIAN_POINT('Ctrl Pts',(17.3674340003121,-16.7856336283223,
21.8951326731846));
#205624=CARTESIAN_POINT('Ctrl Pts',(17.4398582963668,-16.7432000428021,
21.8993079437988));
#205625=CARTESIAN_POINT('Ctrl Pts',(17.5126335322061,-16.7005608407393,
21.9035034461398));
#205626=CARTESIAN_POINT('Ctrl Pts',(17.5875985480893,-16.6614751468356,
21.9076989484807));
#205627=CARTESIAN_POINT('Ctrl Pts',(17.6643699161775,-16.6261686467455,
21.9118944508217));
#205628=CARTESIAN_POINT('Ctrl Pts',(17.7406375998076,-16.5910937868593,
21.9160624271542));
#205629=CARTESIAN_POINT('Ctrl Pts',(17.8186875806148,-16.5597488751243,
21.9202304034868));
#205630=CARTESIAN_POINT('Ctrl Pts',(17.8981189457526,-16.532309345567,21.9243983798194));
#205631=CARTESIAN_POINT('Ctrl Pts',(17.9775252548952,-16.5048784715921,
21.9285650413968));
#205632=CARTESIAN_POINT('Ctrl Pts',(18.0583116477558,-16.4813506834989,
21.9327317029742));
#205633=CARTESIAN_POINT('Ctrl Pts',(18.1400589392981,-16.4618526115082,
21.9368983645517));
#205634=CARTESIAN_POINT('Ctrl Pts',(18.2218050628271,-16.442354818108,21.9410649665955));
#205635=CARTESIAN_POINT('Ctrl Pts',(18.3045116092594,-16.426886732127,21.9452315686392));
#205636=CARTESIAN_POINT('Ctrl Pts',(18.3877473464946,-16.4155242757045,
21.949398170683));
#205637=CARTESIAN_POINT('Ctrl Pts',(18.4719862643408,-16.4040248757484,
21.9536149897912));
#205638=CARTESIAN_POINT('Ctrl Pts',(18.5567667383605,-16.3967308160666,
21.9578318088995));
#205639=CARTESIAN_POINT('Ctrl Pts',(18.6416363028403,-16.3936667637997,
21.9620486280077));
#205640=CARTESIAN_POINT('Ctrl Pts',(18.7256174343069,-16.3906347866968,
21.9662213045387));
#205641=CARTESIAN_POINT('Ctrl Pts',(18.8096853344826,-16.3917446006535,
21.9703939810697));
#205642=CARTESIAN_POINT('Ctrl Pts',(18.8934033137617,-16.3969675963773,
21.9745666576007));
#205643=CARTESIAN_POINT('Ctrl Pts',(18.9784497667459,-16.4022734728939,
21.9788055479976));
#205644=CARTESIAN_POINT('Ctrl Pts',(19.0631346044503,-16.4118241506696,
21.9830444383944));
#205645=CARTESIAN_POINT('Ctrl Pts',(19.1470091266727,-16.4255353829343,
21.9872833287913));
#205646=CARTESIAN_POINT('Ctrl Pts',(19.2308836488952,-16.439246615199,21.9915222191882));
#205647=CARTESIAN_POINT('Ctrl Pts',(19.3139473893182,-16.4571182338667,
21.9957611095851));
#205648=CARTESIAN_POINT('Ctrl Pts',(19.3957679668415,-16.4790133121946,
21.9999999999819));
#205649=CARTESIAN_POINT('',(18.0722627314314,-16.4790050975816,22.));
#205650=CARTESIAN_POINT('Origin',(18.734,-18.952,22.));
#205651=CARTESIAN_POINT('',(16.1765333501007,-18.9488555363839,21.8332901097715));
#205652=CARTESIAN_POINT('Ctrl Pts',(16.1765333501007,-18.9488555363839,
21.8332901097715));
#205653=CARTESIAN_POINT('Ctrl Pts',(16.1744954273233,-18.6834061757001,
21.8464681376205));
#205654=CARTESIAN_POINT('Ctrl Pts',(16.3345563979949,-17.5672065717878,
21.90203810103));
#205655=CARTESIAN_POINT('Ctrl Pts',(17.2488902483963,-16.6993275322964,
21.9576080644395));
#205656=CARTESIAN_POINT('Ctrl Pts',(18.0722627314314,-16.4790050975816,
22.));
#205657=CARTESIAN_POINT('Ctrl Pts',(20.2910035915388,-20.9788220864065,
21.5499225011608));
#205658=CARTESIAN_POINT('Ctrl Pts',(19.9247545666378,-21.2588470681592,
21.5727725274258));
#205659=CARTESIAN_POINT('Ctrl Pts',(18.672556959445,-21.7916141725372,21.6380144892512));
#205660=CARTESIAN_POINT('Ctrl Pts',(16.6739013977444,-20.9887406839414,
21.7324703587881));
#205661=CARTESIAN_POINT('Ctrl Pts',(16.1810511496244,-19.5373209132916,
21.80407620206));
#205662=CARTESIAN_POINT('Ctrl Pts',(16.1765333501007,-18.9488555363839,
21.8332901097715));
#205663=CARTESIAN_POINT('Origin',(18.734,19.211,-1.76670989022852));
#205664=CARTESIAN_POINT('',(16.1740007447408,19.2090472910618,21.7667098902285));
#205665=CARTESIAN_POINT('Ctrl Pts',(20.2957383339893,17.178031980842,21.4832513393832));
#205666=CARTESIAN_POINT('Ctrl Pts',(20.245887425011,17.1392615823117,21.4864046693096));
#205667=CARTESIAN_POINT('Ctrl Pts',(19.5043144389604,16.6078642735819,21.5319499347965));
#205668=CARTESIAN_POINT('Ctrl Pts',(17.5061735829933,16.443821090153,21.6198871358438));
#205669=CARTESIAN_POINT('Ctrl Pts',(16.2398215703271,18.0973737800013,21.7112199895325));
#205670=CARTESIAN_POINT('Ctrl Pts',(16.1708575106781,19.0777088474958,21.7601609076608));
#205671=CARTESIAN_POINT('Ctrl Pts',(16.1719918287103,19.2090457587065,21.7667098902285));
#205672=CARTESIAN_POINT('',(19.3957680159044,21.6839866746762,21.9999999999818));
#205673=CARTESIAN_POINT('Ctrl Pts',(16.1740007447408,19.2090472910617,21.7667098902285));
#205674=CARTESIAN_POINT('Ctrl Pts',(16.1739377131957,19.291681576866,21.770833628557));
#205675=CARTESIAN_POINT('Ctrl Pts',(16.1778799213038,19.3744638154111,21.7749573668856));
#205676=CARTESIAN_POINT('Ctrl Pts',(16.1858438026722,19.4569674653686,21.7790811052141));
#205677=CARTESIAN_POINT('Ctrl Pts',(16.1937978799175,19.539369547271,21.7831997669178));
#205678=CARTESIAN_POINT('Ctrl Pts',(16.2057637505312,19.6214932533812,21.7873184286214));
#205679=CARTESIAN_POINT('Ctrl Pts',(16.2217058123253,19.7029125070335,21.7914370903251));
#205680=CARTESIAN_POINT('Ctrl Pts',(16.237637182478,19.7842771563645,21.795552989823));
#205681=CARTESIAN_POINT('Ctrl Pts',(16.257539363199,19.864937827131,21.799668889321));
#205682=CARTESIAN_POINT('Ctrl Pts',(16.2813251278132,19.9444752697558,21.803784788819));
#205683=CARTESIAN_POINT('Ctrl Pts',(16.3051025310591,20.0239847527225,21.807899241462));
#205684=CARTESIAN_POINT('Ctrl Pts',(16.3327606729939,20.1023713378542,21.812013694105));
#205685=CARTESIAN_POINT('Ctrl Pts',(16.3641619718452,20.1792291672488,21.816128146748));
#205686=CARTESIAN_POINT('Ctrl Pts',(16.3955622525032,20.2560845045131,21.820242465979));
#205687=CARTESIAN_POINT('Ctrl Pts',(16.4307052681111,20.331410746752,21.8243567852101));
#205688=CARTESIAN_POINT('Ctrl Pts',(16.4694052055202,20.4048217692834,21.8284711044412));
#205689=CARTESIAN_POINT('Ctrl Pts',(16.5081407935446,20.4783004184906,21.8325892138079));
#205690=CARTESIAN_POINT('Ctrl Pts',(16.5504396244287,20.5498599054295,21.8367073231746));
#205691=CARTESIAN_POINT('Ctrl Pts',(16.596070140308,20.6191391674964,21.8408254325413));
#205692=CARTESIAN_POINT('Ctrl Pts',(16.6417225473624,20.6884516661905,21.8449455175651));
#205693=CARTESIAN_POINT('Ctrl Pts',(16.6907095403228,20.7554813807654,21.849065602589));
#205694=CARTESIAN_POINT('Ctrl Pts',(16.7427579777409,20.819898756538,21.8531856876128));
#205695=CARTESIAN_POINT('Ctrl Pts',(16.7948924451882,20.88442260676,21.8573125826592));
#205696=CARTESIAN_POINT('Ctrl Pts',(16.8500981442698,20.9463251442536,21.8614394777056));
#205697=CARTESIAN_POINT('Ctrl Pts',(16.9080639888335,21.0053125934813,21.865566372752));
#205698=CARTESIAN_POINT('Ctrl Pts',(16.9486676888643,21.0466319033619,21.8684571649036));
#205699=CARTESIAN_POINT('Ctrl Pts',(16.990624926523,21.0865216582628,21.8713479570551));
#205700=CARTESIAN_POINT('Ctrl Pts',(17.0338195605382,21.124893015106,21.8742387492067));
#205701=CARTESIAN_POINT('Ctrl Pts',(17.096294549636,21.1803918092294,21.8784198752255));
#205702=CARTESIAN_POINT('Ctrl Pts',(17.1616053008015,21.2329308852276,21.8826010012442));
#205703=CARTESIAN_POINT('Ctrl Pts',(17.2294394909469,21.2822068159887,21.886782127263));
#205704=CARTESIAN_POINT('Ctrl Pts',(17.2971786580471,21.3314137203636,21.8909573963043));
#205705=CARTESIAN_POINT('Ctrl Pts',(17.3674338732044,21.377366290339,21.8951326653455));
#205706=CARTESIAN_POINT('Ctrl Pts',(17.4398581404809,21.4197998658639,21.8993079343868));
#205707=CARTESIAN_POINT('Ctrl Pts',(17.5126333816213,21.462439077932,21.9035034371199));
#205708=CARTESIAN_POINT('Ctrl Pts',(17.5875984040009,21.5015247814357,21.907698939853));
#205709=CARTESIAN_POINT('Ctrl Pts',(17.6643697795486,21.5368312904201,21.9118944425862));
#205710=CARTESIAN_POINT('Ctrl Pts',(17.7406374344996,21.5719061425448,21.916062417336));
#205711=CARTESIAN_POINT('Ctrl Pts',(17.8186873858889,21.603251049355,21.9202303920859));
#205712=CARTESIAN_POINT('Ctrl Pts',(17.8981187211547,21.6306905768457,21.9243983668358));
#205713=CARTESIAN_POINT('Ctrl Pts',(17.9775250004187,21.6581214487492,21.9285650268302));
#205714=CARTESIAN_POINT('Ctrl Pts',(18.0583113629463,21.681649237629,21.9327316868246));
#205715=CARTESIAN_POINT('Ctrl Pts',(18.1400586239765,21.7011473132823,21.936898346819));
#205716=CARTESIAN_POINT('Ctrl Pts',(18.2218047170262,21.720645110353,21.9410649472815));
#205717=CARTESIAN_POINT('Ctrl Pts',(18.3045112328003,21.7361132028771,21.9452315477439));
#205718=CARTESIAN_POINT('Ctrl Pts',(18.3877469394689,21.7474756687327,21.9493981482063));
#205719=CARTESIAN_POINT('Ctrl Pts',(18.471985895769,21.7589750877077,21.9536149691876));
#205720=CARTESIAN_POINT('Ctrl Pts',(18.5567664092282,21.7662691624329,21.9578317901689));
#205721=CARTESIAN_POINT('Ctrl Pts',(18.6416360132955,21.7693332257468,21.9620486111502));
#205722=CARTESIAN_POINT('Ctrl Pts',(18.7256171152011,21.7723652112997,21.9662212861195));
#205723=CARTESIAN_POINT('Ctrl Pts',(18.8096849858173,21.7712554086671,21.9703939610888));
#205724=CARTESIAN_POINT('Ctrl Pts',(18.8934029358148,21.766032427202,21.9745666360581));
#205725=CARTESIAN_POINT('Ctrl Pts',(18.9784494629181,21.7607265586906,21.9788055300454));
#205726=CARTESIAN_POINT('Ctrl Pts',(19.0631343741421,21.7511758815698,21.9830444240327));
#205727=CARTESIAN_POINT('Ctrl Pts',(19.1470089679579,21.7374646430113,21.98728331802));
#205728=CARTESIAN_POINT('Ctrl Pts',(19.2308835617738,21.7237534044529,21.9915222120073));
#205729=CARTESIAN_POINT('Ctrl Pts',(19.3139473718607,21.7058817725444,21.9957611059945));
#205730=CARTESIAN_POINT('Ctrl Pts',(19.3957680159044,21.6839866746762,21.9999999999818));
#205731=CARTESIAN_POINT('',(18.0722627314313,21.6839949024184,22.));
#205732=CARTESIAN_POINT('Origin',(18.734,19.211,22.));
#205733=CARTESIAN_POINT('',(16.1765333526442,19.2141444406009,21.8332901097715));
#205734=CARTESIAN_POINT('Ctrl Pts',(16.1765333526442,19.2141444406009,21.8332901097715));
#205735=CARTESIAN_POINT('Ctrl Pts',(16.1744954308812,19.4795937966726,21.8464681376205));
#205736=CARTESIAN_POINT('Ctrl Pts',(16.3345564048251,20.5957933867983,21.90203810103));
#205737=CARTESIAN_POINT('Ctrl Pts',(17.2488902483962,21.4636724677035,21.9576080644395));
#205738=CARTESIAN_POINT('Ctrl Pts',(18.0722627314313,21.6839949024184,22.));
#205739=CARTESIAN_POINT('Ctrl Pts',(20.2910035798173,17.1841778967012,21.5499225020685));
#205740=CARTESIAN_POINT('Ctrl Pts',(19.9247545573495,16.9041529176524,21.5727725280309));
#205741=CARTESIAN_POINT('Ctrl Pts',(18.6725569530959,16.3713858130565,21.6380144895538));
#205742=CARTESIAN_POINT('Ctrl Pts',(16.6739013896572,17.1742593445012,21.7324703587881));
#205743=CARTESIAN_POINT('Ctrl Pts',(16.1810511499193,18.6256790739174,21.80407620206));
#205744=CARTESIAN_POINT('Ctrl Pts',(16.1765333526442,19.2141444406009,21.8332901097715));
#205745=CARTESIAN_POINT('Origin',(-18.734,19.211,-1.76670989022852));
#205746=CARTESIAN_POINT('',(-21.2939992552807,19.2090473192565,21.7667098902285));
#205747=CARTESIAN_POINT('Ctrl Pts',(-17.1722616694474,17.1780320626177,
21.4832513372676));
#205748=CARTESIAN_POINT('Ctrl Pts',(-17.2221125877366,17.1392616549198,
21.4864046678992));
#205749=CARTESIAN_POINT('Ctrl Pts',(-17.9636855620214,16.6078643332858,
21.5319499340913));
#205750=CARTESIAN_POINT('Ctrl Pts',(-19.9618263432431,16.4438210470481,
21.6198871358438));
#205751=CARTESIAN_POINT('Ctrl Pts',(-21.2281784392051,18.0973738826004,
21.7112199895325));
#205752=CARTESIAN_POINT('Ctrl Pts',(-21.2971424588611,19.0777088858588,
21.7601609076608));
#205753=CARTESIAN_POINT('Ctrl Pts',(-21.2960081347233,19.2090457869513,
21.7667098902285));
#205754=CARTESIAN_POINT('',(-18.0722321029123,21.6839867064714,21.999999999982));
#205755=CARTESIAN_POINT('Ctrl Pts',(-21.2939992552807,19.2090473192565,
21.7667098902285));
#205756=CARTESIAN_POINT('Ctrl Pts',(-21.2940622859128,19.291681601191,21.7708336286224));
#205757=CARTESIAN_POINT('Ctrl Pts',(-21.2901200772654,19.3744638362772,
21.7749573670163));
#205758=CARTESIAN_POINT('Ctrl Pts',(-21.2821561956048,19.456967483218,21.7790811054102));
#205759=CARTESIAN_POINT('Ctrl Pts',(-21.2742021181198,19.5393695615683,
21.7831997671522));
#205760=CARTESIAN_POINT('Ctrl Pts',(-21.2622362475653,19.621493264571,21.7873184288942));
#205761=CARTESIAN_POINT('Ctrl Pts',(-21.2462941860021,19.7029125155758,
21.7914370906363));
#205762=CARTESIAN_POINT('Ctrl Pts',(-21.2303628161442,19.7842771619339,
21.795552990156));
#205763=CARTESIAN_POINT('Ctrl Pts',(-21.2104606359213,19.8649378301924,
21.7996688896757));
#205764=CARTESIAN_POINT('Ctrl Pts',(-21.1866748718834,19.9444752707705,
21.8037847891954));
#205765=CARTESIAN_POINT('Ctrl Pts',(-21.1628974693084,20.0239847513738,
21.8078992418438));
#205766=CARTESIAN_POINT('Ctrl Pts',(-21.1352393281534,20.102371334612,21.8120136944921));
#205767=CARTESIAN_POINT('Ctrl Pts',(-21.1038380300699,20.1792291625614,
21.8161281471405));
#205768=CARTESIAN_POINT('Ctrl Pts',(-21.0724377503042,20.2560844980759,
21.8202424663606));
#205769=CARTESIAN_POINT('Ctrl Pts',(-21.0372947356062,20.3314107390252,
21.8243567855807));
#205770=CARTESIAN_POINT('Ctrl Pts',(-20.9985947990105,20.404821760689,21.8284711048008));
#205771=CARTESIAN_POINT('Ctrl Pts',(-20.959859212032,20.4783004085882,21.8325892141319));
#205772=CARTESIAN_POINT('Ctrl Pts',(-20.9175603821396,20.5498598946646,
21.836707323463));
#205773=CARTESIAN_POINT('Ctrl Pts',(-20.8719298670911,20.6191391562625,
21.8408254327941));
#205774=CARTESIAN_POINT('Ctrl Pts',(-20.8262774610213,20.6884516542547,
21.8449455177684));
#205775=CARTESIAN_POINT('Ctrl Pts',(-20.7772904689067,20.7554813685366,
21.8490656027427));
#205776=CARTESIAN_POINT('Ctrl Pts',(-20.7252420320998,20.8198987443587,
21.8531856877171));
#205777=CARTESIAN_POINT('Ctrl Pts',(-20.6731075655348,20.884422594296,21.8573125826926));
#205778=CARTESIAN_POINT('Ctrl Pts',(-20.617901867132,20.9463251318754,21.861439477668));
#205779=CARTESIAN_POINT('Ctrl Pts',(-20.5599360229587,21.0053125814812,
21.8655663726435));
#205780=CARTESIAN_POINT('Ctrl Pts',(-20.5193323219955,21.0466318928538,
21.8684571648312));
#205781=CARTESIAN_POINT('Ctrl Pts',(-20.477375083183,21.0865216493047,21.871347957019));
#205782=CARTESIAN_POINT('Ctrl Pts',(-20.4341804477789,21.1248930077176,
21.8742387492067));
#205783=CARTESIAN_POINT('Ctrl Pts',(-20.3717054008517,21.1803918536987,
21.8784198790135));
#205784=CARTESIAN_POINT('Ctrl Pts',(-20.3063945881463,21.2329309746761,
21.8826010088204));
#205785=CARTESIAN_POINT('Ctrl Pts',(-20.2385603336045,21.2822069434375,
21.8867821386272));
#205786=CARTESIAN_POINT('Ctrl Pts',(-20.1708211017769,21.3314138860656,
21.8909574114772));
#205787=CARTESIAN_POINT('Ctrl Pts',(-20.1005658190123,21.3773664872955,
21.8951326843272));
#205788=CARTESIAN_POINT('Ctrl Pts',(-20.0281414820515,21.4198000870231,
21.8993079571772));
#205789=CARTESIAN_POINT('Ctrl Pts',(-19.9553662537474,21.4624392748643,
21.9035034589607));
#205790=CARTESIAN_POINT('Ctrl Pts',(-19.8804012470982,21.5015249551222,
21.9076989607443));
#205791=CARTESIAN_POINT('Ctrl Pts',(-19.8036298896135,21.5368314425696,
21.9118944625278));
#205792=CARTESIAN_POINT('Ctrl Pts',(-19.7273621652182,21.571906313488,21.9160624411101));
#205793=CARTESIAN_POINT('Ctrl Pts',(-19.6493121425953,21.6032512322234,
21.9202304196923));
#205794=CARTESIAN_POINT('Ctrl Pts',(-19.5698807349969,21.6306907647179,
21.9243983982746));
#205795=CARTESIAN_POINT('Ctrl Pts',(-19.4904743833841,21.6581216416371,
21.9285650621022));
#205796=CARTESIAN_POINT('Ctrl Pts',(-19.4096879474075,21.6816494286122,
21.9327317259298));
#205797=CARTESIAN_POINT('Ctrl Pts',(-19.3279406124946,21.7011474953965,
21.9368983897574));
#205798=CARTESIAN_POINT('Ctrl Pts',(-19.2461944456416,21.7206452835795,
21.941064994049));
#205799=CARTESIAN_POINT('Ctrl Pts',(-19.1634878556314,21.7361133602598,
21.9452315983405));
#205800=CARTESIAN_POINT('Ctrl Pts',(-19.0802520749481,21.7474758032739,
21.9493982026321));
#205801=CARTESIAN_POINT('Ctrl Pts',(-18.9960132117624,21.7589751761959,
21.9536150190779));
#205802=CARTESIAN_POINT('Ctrl Pts',(-18.9112327938041,21.7662692144946,
21.9578318355238));
#205803=CARTESIAN_POINT('Ctrl Pts',(-18.8263632855961,21.7693332510589,
21.9620486519696));
#205804=CARTESIAN_POINT('Ctrl Pts',(-18.742382112111,21.7723652161511,21.9662213307204));
#205805=CARTESIAN_POINT('Ctrl Pts',(-18.6583141699189,21.7712553860981,
21.9703940094712));
#205806=CARTESIAN_POINT('Ctrl Pts',(-18.5745961490186,21.7660323701065,
21.9745666882221));
#205807=CARTESIAN_POINT('Ctrl Pts',(-18.489549801391,21.7607264822116,21.9788055735154));
#205808=CARTESIAN_POINT('Ctrl Pts',(-18.404865068191,21.7511758035055,21.9830444588087));
#205809=CARTESIAN_POINT('Ctrl Pts',(-18.3209906477349,21.7374645801874,
21.987283344102));
#205810=CARTESIAN_POINT('Ctrl Pts',(-18.2371162272788,21.7237533568693,
21.9915222293954));
#205811=CARTESIAN_POINT('Ctrl Pts',(-18.15405258588,21.7058817570232,21.9957611146887));
#205812=CARTESIAN_POINT('Ctrl Pts',(-18.0722321029123,21.6839867064714,
21.999999999982));
#205813=CARTESIAN_POINT('',(-19.3957372685686,21.6839949024184,22.));
#205814=CARTESIAN_POINT('Origin',(-18.734,19.211,22.));
#205815=CARTESIAN_POINT('',(-21.2914665292272,19.2141433713253,21.8332901097715));
#205816=CARTESIAN_POINT('Ctrl Pts',(-21.2914665292272,19.2141433713253,
21.8332901097715));
#205817=CARTESIAN_POINT('Ctrl Pts',(-21.2935044038853,19.4795925132556,
21.8464681376205));
#205818=CARTESIAN_POINT('Ctrl Pts',(-21.1334432779756,20.5957914633395,
21.90203810103));
#205819=CARTESIAN_POINT('Ctrl Pts',(-20.2191097516038,21.4636724677035,
21.9576080644395));
#205820=CARTESIAN_POINT('Ctrl Pts',(-19.3957372685686,21.6839949024184,
22.));
#205821=CARTESIAN_POINT('Ctrl Pts',(-17.1769962058593,17.1841776921994,
21.549922496891));
#205822=CARTESIAN_POINT('Ctrl Pts',(-17.5432452683728,16.9041525164483,
21.5727725245792));
#205823=CARTESIAN_POINT('Ctrl Pts',(-18.7954430079984,16.371385010207,21.6380144878279));
#205824=CARTESIAN_POINT('Ctrl Pts',(-20.7940989859098,17.1742606647151,
21.7324703587881));
#205825=CARTESIAN_POINT('Ctrl Pts',(-21.2869488363774,18.6256784793645,
21.80407620206));
#205826=CARTESIAN_POINT('Ctrl Pts',(-21.2914665292272,19.2141433713253,
21.8332901097715));
#205827=CARTESIAN_POINT('Origin',(26.8463464956315,10.1295,7.));
#205828=CARTESIAN_POINT('',(18.7216535115672,10.1295873228123,12.0987228108905));
#205829=CARTESIAN_POINT('Ctrl Pts',(18.9778214339751,14.6099559957068,9.43455988473872));
#205830=CARTESIAN_POINT('Ctrl Pts',(18.9452723572074,14.27750379166,10.0450302603514));
#205831=CARTESIAN_POINT('Ctrl Pts',(18.8739413988038,13.2738298860402,11.2340275217565));
#205832=CARTESIAN_POINT('Ctrl Pts',(18.7885520913344,11.5585268032384,12.0007214198279));
#205833=CARTESIAN_POINT('Ctrl Pts',(18.7357118606328,10.4298968038467,12.0989142199688));
#205834=CARTESIAN_POINT('Ctrl Pts',(18.7216535115672,10.1295873228123,12.0987228108905));
#205835=CARTESIAN_POINT('',(17.734,14.4077184404108,4.2257166734219));
#205836=CARTESIAN_POINT('Ctrl Pts',(18.7216535043684,10.1295871737727,12.0989999992548));
#205837=CARTESIAN_POINT('Ctrl Pts',(18.7147113410273,9.98128307520553,12.0990025346986));
#205838=CARTESIAN_POINT('Ctrl Pts',(18.7077691776862,9.8329749558716,12.0925306029392));
#205839=CARTESIAN_POINT('Ctrl Pts',(18.7008270143451,9.68523504562768,12.0796092025191));
#205840=CARTESIAN_POINT('Ctrl Pts',(18.6938850789891,9.53749998725783,12.0666882264461));
#205841=CARTESIAN_POINT('Ctrl Pts',(18.6869431436331,9.3903334278217,12.0473182361383));
#205842=CARTESIAN_POINT('Ctrl Pts',(18.6800012082771,9.244302805183,12.0215761396486));
#205843=CARTESIAN_POINT('Ctrl Pts',(18.6730576317816,9.0982376595178,11.9958279574827));
#205844=CARTESIAN_POINT('Ctrl Pts',(18.6661140552862,8.95330931088689,11.9637047165393));
#205845=CARTESIAN_POINT('Ctrl Pts',(18.6591704787908,8.81007598055744,11.9253346340039));
#205846=CARTESIAN_POINT('Ctrl Pts',(18.6552746238124,8.72971159148627,11.9038062073836));
#205847=CARTESIAN_POINT('Ctrl Pts',(18.6513787688341,8.64988059910993,11.8803121723026));
#205848=CARTESIAN_POINT('Ctrl Pts',(18.6474829138558,8.57067970016459,11.8548821069951));
#205849=CARTESIAN_POINT('Ctrl Pts',(18.6405493036326,8.4297226661706,11.8096231941828));
#205850=CARTESIAN_POINT('Ctrl Pts',(18.6336156934094,8.29071373380833,11.7582135060853));
#205851=CARTESIAN_POINT('Ctrl Pts',(18.6266820831862,8.15419024687287,11.7008459216614));
#205852=CARTESIAN_POINT('Ctrl Pts',(18.6197497891957,8.01769267669309,11.6434892275371));
#205853=CARTESIAN_POINT('Ctrl Pts',(18.6128174952052,7.88367991517738,11.5801770216112));
#205854=CARTESIAN_POINT('Ctrl Pts',(18.6058852012147,7.75266950923779,11.5111503874492));
#205855=CARTESIAN_POINT('Ctrl Pts',(18.5989526626174,7.62165448058108,11.4421213176745));
#205856=CARTESIAN_POINT('Ctrl Pts',(18.5920201240202,7.49364231349697,11.3673775673167));
#205857=CARTESIAN_POINT('Ctrl Pts',(18.5850875854229,7.36912660488231,11.2872065170139));
#205858=CARTESIAN_POINT('Ctrl Pts',(18.5781554218558,7.24461763220445,11.2070398037311));
#205859=CARTESIAN_POINT('Ctrl Pts',(18.5712232582886,7.12360501695346,11.121446557744));
#205860=CARTESIAN_POINT('Ctrl Pts',(18.5642910947215,7.00655398674484,11.030757893783));
#205861=CARTESIAN_POINT('Ctrl Pts',(18.5573573897854,6.8894769301988,10.9400490651659));
#205862=CARTESIAN_POINT('Ctrl Pts',(18.5504236848492,6.77636348017962,10.8442427572896));
#205863=CARTESIAN_POINT('Ctrl Pts',(18.5434899799131,6.6676468407924,10.7437112207119));
#205864=CARTESIAN_POINT('Ctrl Pts',(18.5393724095913,6.60308562684493,10.6840107178447));
#205865=CARTESIAN_POINT('Ctrl Pts',(18.5352548392694,6.54007433979697,10.622644599298));
#205866=CARTESIAN_POINT('Ctrl Pts',(18.5311372689476,6.47869775743707,10.5596971761229));
#205867=CARTESIAN_POINT('Ctrl Pts',(18.5242037115753,6.37534601797689,10.4537003051742));
#205868=CARTESIAN_POINT('Ctrl Pts',(18.5172701542029,6.27659580949282,10.3431810703944));
#205869=CARTESIAN_POINT('Ctrl Pts',(18.5103365968306,6.18283159101337,10.2285615170703));
#205870=CARTESIAN_POINT('Ctrl Pts',(18.5034043559565,6.089085175867,10.113963726953));
#205871=CARTESIAN_POINT('Ctrl Pts',(18.4964721150824,6.0003230711042,9.99526742733144));
#205872=CARTESIAN_POINT('Ctrl Pts',(18.4895398742083,5.91688967035563,9.87292798562261));
#205873=CARTESIAN_POINT('Ctrl Pts',(18.4826073886049,5.83345332415193,9.75058422495596));
#205874=CARTESIAN_POINT('Ctrl Pts',(18.4756749030014,5.75534624741186,9.62459733606426));
#205875=CARTESIAN_POINT('Ctrl Pts',(18.4687424173979,5.68286999196541,9.49545237815638));
#205876=CARTESIAN_POINT('Ctrl Pts',(18.4618103066269,5.61039765523575,9.36631440298387));
#205877=CARTESIAN_POINT('Ctrl Pts',(18.4548781958558,5.5435556915652,9.23401898922316));
#205878=CARTESIAN_POINT('Ctrl Pts',(18.4479460850847,5.48260010633888,9.09907655369981));
#205879=CARTESIAN_POINT('Ctrl Pts',(18.4410124321748,5.42163096074452,8.96410409846483));
#205880=CARTESIAN_POINT('Ctrl Pts',(18.434078779265,5.36655094628959,8.82648374621635));
#205881=CARTESIAN_POINT('Ctrl Pts',(18.4271451263551,5.3175685098331,8.68674726439385));
#205882=CARTESIAN_POINT('Ctrl Pts',(18.4230272922499,5.28847828134614,8.6037590245624));
#205883=CARTESIAN_POINT('Ctrl Pts',(18.4189094581446,5.26153778917509,8.52002479046549));
#205884=CARTESIAN_POINT('Ctrl Pts',(18.4147916240394,5.23678246616714,8.43565878053404));
#205885=CARTESIAN_POINT('Ctrl Pts',(18.4078580499257,5.19509966341243,8.29360400912006));
#205886=CARTESIAN_POINT('Ctrl Pts',(18.400924475812,5.15960044824281,8.1497081866558));
#205887=CARTESIAN_POINT('Ctrl Pts',(18.3939909016982,5.13042688503271,8.00452426113619));
#205888=CARTESIAN_POINT('Ctrl Pts',(18.3870586444984,5.10125886284241,7.85936791082228));
#205889=CARTESIAN_POINT('Ctrl Pts',(18.3801263872986,5.07841416062936,7.71292426949538));
#205890=CARTESIAN_POINT('Ctrl Pts',(18.3731941300988,5.06198383767688,7.56575696601455));
#205891=CARTESIAN_POINT('Ctrl Pts',(18.3662616289537,5.04555293654322,7.41858448373312));
#205892=CARTESIAN_POINT('Ctrl Pts',(18.3593291278085,5.03553690634891,7.27068861649685));
#205893=CARTESIAN_POINT('Ctrl Pts',(18.3523966266634,5.03197504813123,7.12263916615529));
#205894=CARTESIAN_POINT('Ctrl Pts',(18.3454645008326,5.02841338274678,6.97459773097103));
#205895=CARTESIAN_POINT('Ctrl Pts',(18.3385323750019,5.0313051971733,6.82640305983149));
#205896=CARTESIAN_POINT('Ctrl Pts',(18.3316002491711,5.04063767405535,6.67862603157506));
#205897=CARTESIAN_POINT('Ctrl Pts',(18.3246665820787,5.0499722258837,6.53081614715388));
#205898=CARTESIAN_POINT('Ctrl Pts',(18.3177329149862,5.06575028063441,6.38342442119573));
#205899=CARTESIAN_POINT('Ctrl Pts',(18.3107992478938,5.08790700112659,6.23701832675314));
#205900=CARTESIAN_POINT('Ctrl Pts',(18.3066814916396,5.10106540246934,6.15007088566497));
#205901=CARTESIAN_POINT('Ctrl Pts',(18.3025637353854,5.11647251715666,6.06347097260691));
#205902=CARTESIAN_POINT('Ctrl Pts',(18.2984459791312,5.13410616806531,5.97733609437465));
#205903=CARTESIAN_POINT('Ctrl Pts',(18.2915124969837,5.16379772730853,5.83230209924856));
#205904=CARTESIAN_POINT('Ctrl Pts',(18.2845790148362,5.19981494209206,5.6885370247223));
#205905=CARTESIAN_POINT('Ctrl Pts',(18.2776455326886,5.24202440558095,5.54659595639818));
#205906=CARTESIAN_POINT('Ctrl Pts',(18.2707133673131,5.28422585286128,5.4046818448063));
#205907=CARTESIAN_POINT('Ctrl Pts',(18.2637812019376,5.33261710836953,5.26459136499318));
#205908=CARTESIAN_POINT('Ctrl Pts',(18.256849036562,5.38701469658392,5.12686515517903));
#205909=CARTESIAN_POINT('Ctrl Pts',(18.2499166261359,5.44141420774157,4.98913407677243));
#205910=CARTESIAN_POINT('Ctrl Pts',(18.2429842157098,5.5018203581369,4.85376774430463));
#205911=CARTESIAN_POINT('Ctrl Pts',(18.2360518052837,5.5680010490493,4.72128801282926));
#205912=CARTESIAN_POINT('Ctrl Pts',(18.2291197693284,5.63417816505214,4.58881543756594));
#205913=CARTESIAN_POINT('Ctrl Pts',(18.2221877333731,5.70612904882591,4.45922944662038));
#205914=CARTESIAN_POINT('Ctrl Pts',(18.2152556974179,5.78357504674778,4.33302844021544));
#205915=CARTESIAN_POINT('Ctrl Pts',(18.2083221181144,5.86103828724344,4.20679933642362));
#205916=CARTESIAN_POINT('Ctrl Pts',(18.201388538811,5.94399891348856,4.08395700490077));
#205917=CARTESIAN_POINT('Ctrl Pts',(18.1944549595075,6.03213390326059,3.96497247635372));
#205918=CARTESIAN_POINT('Ctrl Pts',(18.1903367510793,6.08448179484874,3.8943014611626));
#205919=CARTESIAN_POINT('Ctrl Pts',(18.1862185426512,6.13865425945979,3.82499084626316));
#205920=CARTESIAN_POINT('Ctrl Pts',(18.182100334223,6.19457664874617,3.75713410395105));
#205921=CARTESIAN_POINT('Ctrl Pts',(18.1751666155273,6.28873169768777,3.6428855002175));
#205922=CARTESIAN_POINT('Ctrl Pts',(18.1682328968315,6.38788205597123,3.53272058770171));
#205923=CARTESIAN_POINT('Ctrl Pts',(18.1612991781358,6.49164988118888,3.42706737915953));
#205924=CARTESIAN_POINT('Ctrl Pts',(18.1543667758962,6.59539800474326,3.32143423024503));
#205925=CARTESIAN_POINT('Ctrl Pts',(18.1474343736566,6.7037616146166,3.22031131194666));
#205926=CARTESIAN_POINT('Ctrl Pts',(18.140501971417,6.81632539466401,3.12409042487357));
#205927=CARTESIAN_POINT('Ctrl Pts',(18.133569325952,6.92889312404455,3.02786616186255));
#205928=CARTESIAN_POINT('Ctrl Pts',(18.1266366804871,7.04566106939944,2.93654449155148));
#205929=CARTESIAN_POINT('Ctrl Pts',(18.1197040350221,7.16617974834542,2.85047784845847));
#205930=CARTESIAN_POINT('Ctrl Pts',(18.1127717656245,7.28669188965198,2.76441587412456));
#205931=CARTESIAN_POINT('Ctrl Pts',(18.1058394962268,7.41095408788013,2.68360854794937));
#205932=CARTESIAN_POINT('Ctrl Pts',(18.0989072268292,7.53848670899882,2.60836577959238));
#205933=CARTESIAN_POINT('Ctrl Pts',(18.0919734185825,7.66604764024739,2.53310630858688));
#205934=CARTESIAN_POINT('Ctrl Pts',(18.0850396103359,7.79688016019581,2.46341403160105));
#205935=CARTESIAN_POINT('Ctrl Pts',(18.0781058020892,7.93047824811586,2.39955389828982));
#205936=CARTESIAN_POINT('Ctrl Pts',(18.0739887644978,8.00980382657889,2.36163612495559));
#205937=CARTESIAN_POINT('Ctrl Pts',(18.0698717269063,8.09010394201902,2.32577362636113));
#205938=CARTESIAN_POINT('Ctrl Pts',(18.0657546893148,8.17126896360323,2.29201399661252));
#205939=CARTESIAN_POINT('Ctrl Pts',(18.0588213573683,8.30795560407876,2.2351608068521));
#205940=CARTESIAN_POINT('Ctrl Pts',(18.0518880254217,8.44714343822144,2.18425443098161));
#205941=CARTESIAN_POINT('Ctrl Pts',(18.0449546934752,8.58829824151367,2.13949610229159));
#205942=CARTESIAN_POINT('Ctrl Pts',(18.0380226783627,8.72942623555296,2.09474627446251));
#205943=CARTESIAN_POINT('Ctrl Pts',(18.0310906632502,8.87252013840123,2.0561422639854));
#205944=CARTESIAN_POINT('Ctrl Pts',(18.0241586481377,9.01702957132649,2.02383575981188));
#205945=CARTESIAN_POINT('Ctrl Pts',(18.0172263866156,9.16154414107234,1.99152810725164));
#205946=CARTESIAN_POINT('Ctrl Pts',(18.0102941250934,9.30747401965934,1.96551848432784));
#205947=CARTESIAN_POINT('Ctrl Pts',(18.0033618635713,9.45425707373931,1.94590779758275));
#205948=CARTESIAN_POINT('Ctrl Pts',(17.9964299753957,9.60103222261469,1.92629816699833));
#205949=CARTESIAN_POINT('Ctrl Pts',(17.9894980872201,9.74866012719367,1.9130868258486));
#205950=CARTESIAN_POINT('Ctrl Pts',(17.9825661990445,9.89657192712221,1.9063229869901));
#205951=CARTESIAN_POINT('Ctrl Pts',(17.9756327645019,10.0445167232454,1.89955763925304));
#205952=CARTESIAN_POINT('Ctrl Pts',(17.9686993299592,10.1927452108641,1.89924268284508));
#205953=CARTESIAN_POINT('Ctrl Pts',(17.9617658954166,10.3406862695542,1.90537524840624));
#205954=CARTESIAN_POINT('Ctrl Pts',(17.9576469450799,10.4285737183722,1.90901842594365));
#205955=CARTESIAN_POINT('Ctrl Pts',(17.9535279947433,10.5163597158814,1.9149360686311));
#205956=CARTESIAN_POINT('Ctrl Pts',(17.9494090444066,10.6039249349976,1.92311887266872));
#205957=CARTESIAN_POINT('Ctrl Pts',(17.9424753834828,10.7513283966681,1.93689344724857));
#205958=CARTESIAN_POINT('Ctrl Pts',(17.9355417225589,10.8981569837258,1.9570943475134));
#205959=CARTESIAN_POINT('Ctrl Pts',(17.9286080616351,11.043844383057,1.98364919994901));
#205960=CARTESIAN_POINT('Ctrl Pts',(17.921675718497,11.1895040935834,2.01019900546824));
#205961=CARTESIAN_POINT('Ctrl Pts',(17.914743375359,11.3340227240848,2.04310029455465));
#205962=CARTESIAN_POINT('Ctrl Pts',(17.9078110322209,11.4768428889456,2.08222935268351));
#205963=CARTESIAN_POINT('Ctrl Pts',(17.9008784472619,11.6196680358023,2.12135977575131));
#205964=CARTESIAN_POINT('Ctrl Pts',(17.893945862303,11.760794278772,2.16671831846166));
#205965=CARTESIAN_POINT('Ctrl Pts',(17.887013277344,11.8996776268284,2.2181308916412));
#205966=CARTESIAN_POINT('Ctrl Pts',(17.8800810690987,12.0385534280233,2.26954067108361));
#205967=CARTESIAN_POINT('Ctrl Pts',(17.8731488608534,12.1751862684927,2.32700370709501));
#205968=CARTESIAN_POINT('Ctrl Pts',(17.8662166526081,12.3090504196554,2.3902970846073));
#205969=CARTESIAN_POINT('Ctrl Pts',(17.8592829059654,12.4429442779832,2.45360450820139));
#205970=CARTESIAN_POINT('Ctrl Pts',(17.8523491593228,12.5740679203451,2.52274471727729));
#205971=CARTESIAN_POINT('Ctrl Pts',(17.8454154126802,12.7019180096239,2.59744771936065));
#205972=CARTESIAN_POINT('Ctrl Pts',(17.8412980749529,12.7778368487668,2.64180721281625));
#205973=CARTESIAN_POINT('Ctrl Pts',(17.8371807372257,12.8526018488398,2.68812732988671));
#205974=CARTESIAN_POINT('Ctrl Pts',(17.8330633994984,12.9261120521225,2.73634405352367));
#205975=CARTESIAN_POINT('Ctrl Pts',(17.8261558289376,13.0494385678835,2.8172362325956));
#205976=CARTESIAN_POINT('Ctrl Pts',(17.8192482583768,13.1692774271192,2.90349891677528));
#205977=CARTESIAN_POINT('Ctrl Pts',(17.812340687816,13.2851650747901,2.99480600522892));
#205978=CARTESIAN_POINT('Ctrl Pts',(17.805433747039,13.4010421566397,3.08610476894398));
#205979=CARTESIAN_POINT('Ctrl Pts',(17.7985268062619,13.512968479376,3.18244681517665));
#205980=CARTESIAN_POINT('Ctrl Pts',(17.7916198654848,13.6205122246208,3.28346469846606));
#205981=CARTESIAN_POINT('Ctrl Pts',(17.7847138003811,13.728042335292,3.38446977454133));
#205982=CARTESIAN_POINT('Ctrl Pts',(17.7778077352774,13.8311907337587,3.49014927375184));
#205983=CARTESIAN_POINT('Ctrl Pts',(17.7709016701737,13.929561225329,3.60009769496956));
#205984=CARTESIAN_POINT('Ctrl Pts',(17.7639943665765,14.0279493580916,3.71006583369829));
#205985=CARTESIAN_POINT('Ctrl Pts',(17.7570870629792,14.1215576465777,3.82430417516951));
#205986=CARTESIAN_POINT('Ctrl Pts',(17.7501797593819,14.2100286837041,3.94237238018294));
#205987=CARTESIAN_POINT('Ctrl Pts',(17.7447865062546,14.2791072598717,4.03456055563452));
#205988=CARTESIAN_POINT('Ctrl Pts',(17.7393932531273,14.3450546292517,4.12908289781627));
#205989=CARTESIAN_POINT('Ctrl Pts',(17.734,14.4077184404108,4.2257166734219));
#205990=CARTESIAN_POINT('',(17.734,12.4414757859806,2.45527019889635));
#205991=CARTESIAN_POINT('Origin',(17.734,10.1295,7.));
#205992=CARTESIAN_POINT('',(18.5963464936207,10.1294413854624,12.0988853698432));
#205993=CARTESIAN_POINT('Ctrl Pts',(18.5963464895963,10.1294413021288,12.0986559623714));
#205994=CARTESIAN_POINT('Ctrl Pts',(18.5803708311834,9.78816223566316,12.0988021887428));
#205995=CARTESIAN_POINT('Ctrl Pts',(18.5256132911343,8.61850505157706,11.9829820583334));
#205996=CARTESIAN_POINT('Ctrl Pts',(18.4320738694491,6.76024937160752,11.0980785162391));
#205997=CARTESIAN_POINT('Ctrl Pts',(18.3157282245409,5.23345505271711,9.04320502425034));
#205998=CARTESIAN_POINT('Ctrl Pts',(18.1993825796327,4.8466304876897,6.51259606632921));
#205999=CARTESIAN_POINT('Ctrl Pts',(18.0830369347246,5.6899815760821,4.09545078585546));
#206000=CARTESIAN_POINT('Ctrl Pts',(17.9666912898163,7.56685261371754,2.35466742666588));
#206001=CARTESIAN_POINT('Ctrl Pts',(17.8503456449082,10.0408176861101,1.69542432103654));
#206002=CARTESIAN_POINT('Ctrl Pts',(17.772781881636,11.703188220458,2.0796916608358));
#206003=CARTESIAN_POINT('Ctrl Pts',(17.734,12.4414757859806,2.45527019889635));
#206004=CARTESIAN_POINT('Ctrl Pts',(18.8525174992326,14.6098038194187,9.43447708670712));
#206005=CARTESIAN_POINT('Ctrl Pts',(18.8455850997365,14.5391009597508,9.5645954985597));
#206006=CARTESIAN_POINT('Ctrl Pts',(18.8386527002405,14.4627231589996,9.6916367681177));
#206007=CARTESIAN_POINT('Ctrl Pts',(18.8317203007445,14.3809644182859,9.81511124114998));
#206008=CARTESIAN_POINT('Ctrl Pts',(18.8247881779579,14.2992089410048,9.93858078564965));
#206009=CARTESIAN_POINT('Ctrl Pts',(18.8178560551714,14.2120731373499,10.0584835437482));
#206010=CARTESIAN_POINT('Ctrl Pts',(18.8109239323848,14.1198943495422,10.1743588226824));
#206011=CARTESIAN_POINT('Ctrl Pts',(18.803990345741,14.0276960963278,10.2902585710145));
#206012=CARTESIAN_POINT('Ctrl Pts',(18.7970567590971,13.9304529376542,10.4021288826212));
#206013=CARTESIAN_POINT('Ctrl Pts',(18.7901231724533,13.8285428792875,10.5095416762296));
#206014=CARTESIAN_POINT('Ctrl Pts',(18.7871190496934,13.7843881954961,10.5560805362101));
#206015=CARTESIAN_POINT('Ctrl Pts',(18.7841149269336,13.7393579185255,10.6017830545718));
#206016=CARTESIAN_POINT('Ctrl Pts',(18.7811108041737,13.6934849922401,10.6466165105598));
#206017=CARTESIAN_POINT('Ctrl Pts',(18.7741773221436,13.5876107868587,10.7500916300169));
#206018=CARTESIAN_POINT('Ctrl Pts',(18.7672438401135,13.4772089013386,10.8489706438041));
#206019=CARTESIAN_POINT('Ctrl Pts',(18.7603103580834,13.3627009182632,10.9428686032053));
#206020=CARTESIAN_POINT('Ctrl Pts',(18.7533781928252,13.2482146819651,11.0367487299806));
#206021=CARTESIAN_POINT('Ctrl Pts',(18.7464460275669,13.1296241594456,11.1256494802232));
#206022=CARTESIAN_POINT('Ctrl Pts',(18.7395138623087,13.0073843026661,11.2092259312691));
#206023=CARTESIAN_POINT('Ctrl Pts',(18.7325814519985,12.8851401247099,11.292805336741));
#206024=CARTESIAN_POINT('Ctrl Pts',(18.7256490416884,12.7592466253653,11.3710598770508));
#206025=CARTESIAN_POINT('Ctrl Pts',(18.7187166313782,12.6301884988536,11.4436874363192));
#206026=CARTESIAN_POINT('Ctrl Pts',(18.7117845955379,12.5011373437085,11.5163110724457));
#206027=CARTESIAN_POINT('Ctrl Pts',(18.7048525596975,12.3689221920305,11.5833081744226));
#206028=CARTESIAN_POINT('Ctrl Pts',(18.6979205238572,12.2340531491345,11.6444221430085));
#206029=CARTESIAN_POINT('Ctrl Pts',(18.6909869446661,12.0991540789496,11.7055497180289));
#206030=CARTESIAN_POINT('Ctrl Pts',(18.6840533654749,11.9616002381555,11.7607914059618));
#206031=CARTESIAN_POINT('Ctrl Pts',(18.6771197862838,11.8219231385114,11.8099381409984));
#206032=CARTESIAN_POINT('Ctrl Pts',(18.6730015772777,11.7389617308685,11.839128912643));
#206033=CARTESIAN_POINT('Ctrl Pts',(18.6688833682716,11.6552516632411,11.8661704363264));
#206034=CARTESIAN_POINT('Ctrl Pts',(18.6647651592656,11.5709071450112,11.891027135716));
#206035=CARTESIAN_POINT('Ctrl Pts',(18.6577998246933,11.4282510078553,11.9330685249111));
#206036=CARTESIAN_POINT('Ctrl Pts',(18.650834490121,11.2837317271447,11.9688711473952));
#206037=CARTESIAN_POINT('Ctrl Pts',(18.6438691555487,11.1379071299167,11.9982913140726));
#206038=CARTESIAN_POINT('Ctrl Pts',(18.6369053523104,10.9921145923347,12.0277050127044));
#206039=CARTESIAN_POINT('Ctrl Pts',(18.6299415490721,10.8450176285976,12.0507389918283));
#206040=CARTESIAN_POINT('Ctrl Pts',(18.6229777458338,10.6971847677683,12.0673005638549));
#206041=CARTESIAN_POINT('Ctrl Pts',(18.6160146892149,10.5493677567394,12.0838603602436));
#206042=CARTESIAN_POINT('Ctrl Pts',(18.609051632596,10.4008153280418,12.0939490974492));
#206043=CARTESIAN_POINT('Ctrl Pts',(18.6020885759772,10.2521021089812,12.0975258432767));
#206044=CARTESIAN_POINT('Ctrl Pts',(18.6001745491953,10.2112233541923,12.0985090303568));
#206045=CARTESIAN_POINT('Ctrl Pts',(18.5982605224134,10.1703324708191,12.0990004693845));
#206046=CARTESIAN_POINT('Ctrl Pts',(18.5963464956315,10.1294414271024,12.0989999996636));
#206047=CARTESIAN_POINT('Origin',(-26.8463464956315,10.1295,7.));
#206048=CARTESIAN_POINT('',(-18.7216535115683,10.1294126732152,12.0987227687564));
#206049=CARTESIAN_POINT('Ctrl Pts',(-18.977821433234,5.64904402747702,9.43455986027809));
#206050=CARTESIAN_POINT('Ctrl Pts',(-18.9452723567134,5.9814962272458,10.0450302244706));
#206051=CARTESIAN_POINT('Ctrl Pts',(-18.8739413985567,6.98517016733519,
11.2340275234321));
#206052=CARTESIAN_POINT('Ctrl Pts',(-18.7885520913348,8.70047320199483,
12.0007213768745));
#206053=CARTESIAN_POINT('Ctrl Pts',(-18.7357118606335,9.829103193625,12.0989141769127));
#206054=CARTESIAN_POINT('Ctrl Pts',(-18.7216535115683,10.1294126732152,
12.0987227687564));
#206055=CARTESIAN_POINT('',(-17.734,5.85128156875001,4.22571665929507));
#206056=CARTESIAN_POINT('Ctrl Pts',(-18.7216535043684,10.1294128222767,
12.0989999992548));
#206057=CARTESIAN_POINT('Ctrl Pts',(-18.7147113419131,10.2777169024359,
12.0990025348131));
#206058=CARTESIAN_POINT('Ctrl Pts',(-18.7077691794578,10.4260250034406,
12.0925306047745));
#206059=CARTESIAN_POINT('Ctrl Pts',(-18.7008270170026,10.5737648955722,
12.0796092076618));
#206060=CARTESIAN_POINT('Ctrl Pts',(-18.6938850825327,10.7214999358232,
12.0666882348967));
#206061=CARTESIAN_POINT('Ctrl Pts',(-18.6869431480629,10.8686664773571,
12.0473182494839));
#206062=CARTESIAN_POINT('Ctrl Pts',(-18.680001213593,11.0146970824474,12.021576159457));
#206063=CARTESIAN_POINT('Ctrl Pts',(-18.6730576379768,11.1607622107104,
11.9958279837289));
#206064=CARTESIAN_POINT('Ctrl Pts',(-18.6661140623605,11.3056905422907,
11.9637047507785));
#206065=CARTESIAN_POINT('Ctrl Pts',(-18.6591704867443,11.4489238560583,
11.9253346777721));
#206066=CARTESIAN_POINT('Ctrl Pts',(-18.6552746291148,11.5292883007021,
11.9038062391219));
#206067=CARTESIAN_POINT('Ctrl Pts',(-18.6513787714853,11.6091193479438,
11.8803121893208));
#206068=CARTESIAN_POINT('Ctrl Pts',(-18.6474829138558,11.6883203008384,
11.854882106673));
#206069=CARTESIAN_POINT('Ctrl Pts',(-18.6405493032985,11.8292773417162,
11.8096231916184));
#206070=CARTESIAN_POINT('Ctrl Pts',(-18.6336156927412,11.9682862806913,
11.7582135007032));
#206071=CARTESIAN_POINT('Ctrl Pts',(-18.626682082184,12.1048097739243,11.7008459129224));
#206072=CARTESIAN_POINT('Ctrl Pts',(-18.6197497878564,12.2413073504607,
11.6434892154165));
#206073=CARTESIAN_POINT('Ctrl Pts',(-18.6128174935289,12.3753201180157,
11.5801770055648));
#206074=CARTESIAN_POINT('Ctrl Pts',(-18.6058851992013,12.5063305296346,
11.5111503669682));
#206075=CARTESIAN_POINT('Ctrl Pts',(-18.5989526602658,12.6373455639937,
11.4421212927467));
#206076=CARTESIAN_POINT('Ctrl Pts',(-18.5920201213302,12.7653577364192,
11.3673775374312));
#206077=CARTESIAN_POINT('Ctrl Pts',(-18.5850875823947,12.8898734499727,
11.2872064816948));
#206078=CARTESIAN_POINT('Ctrl Pts',(-18.5781554184894,13.0143824275872,
11.20703976298));
#206079=CARTESIAN_POINT('Ctrl Pts',(-18.5712232545841,13.1353950473725,
11.121446511085));
#206080=CARTESIAN_POINT('Ctrl Pts',(-18.5642910906788,13.2524460816721,
11.0307578407749));
#206081=CARTESIAN_POINT('Ctrl Pts',(-18.5573573854077,13.3695231422555,
10.9400490058497));
#206082=CARTESIAN_POINT('Ctrl Pts',(-18.5504236801366,13.4826365958723,
10.8442426912284));
#206083=CARTESIAN_POINT('Ctrl Pts',(-18.5434899748654,13.5913532383767,
10.7437111475033));
#206084=CARTESIAN_POINT('Ctrl Pts',(-18.5393724062262,13.6559144246746,
10.6840106676712));
#206085=CARTESIAN_POINT('Ctrl Pts',(-18.5352548375869,13.7189256853204,
10.6226445735402));
#206086=CARTESIAN_POINT('Ctrl Pts',(-18.5311372689476,13.7803022426319,
10.5596971760522));
#206087=CARTESIAN_POINT('Ctrl Pts',(-18.5242037116084,13.8836539816517,
10.453700305551));
#206088=CARTESIAN_POINT('Ctrl Pts',(-18.5172701542692,13.9824041897261,
10.3431810712656));
#206089=CARTESIAN_POINT('Ctrl Pts',(-18.51033659693,14.0761684078321,10.2285615184816));
#206090=CARTESIAN_POINT('Ctrl Pts',(-18.5034043560879,14.1699148226197,
10.1139637288865));
#206091=CARTESIAN_POINT('Ctrl Pts',(-18.4964721152459,14.2586769270584,
9.99526742983162));
#206092=CARTESIAN_POINT('Ctrl Pts',(-18.4895398744039,14.3421103275237,
9.87292798873217));
#206093=CARTESIAN_POINT('Ctrl Pts',(-18.4826073888305,14.4255466734673,
9.75058422864091));
#206094=CARTESIAN_POINT('Ctrl Pts',(-18.4756749032572,14.5036537499851,
9.62459734036535));
#206095=CARTESIAN_POINT('Ctrl Pts',(-18.4687424176839,14.5761300052532,
9.49545238311256));
#206096=CARTESIAN_POINT('Ctrl Pts',(-18.4618103069418,14.6486023418167,
9.36631440857343));
#206097=CARTESIAN_POINT('Ctrl Pts',(-18.4548781961996,14.7154443053631,
9.23401899548399));
#206098=CARTESIAN_POINT('Ctrl Pts',(-18.4479460854575,14.7763998905137,
9.09907656066754));
#206099=CARTESIAN_POINT('Ctrl Pts',(-18.4410124325745,14.8373690360505,
8.96410410609937));
#206100=CARTESIAN_POINT('Ctrl Pts',(-18.4340787796916,14.8924490504929,
8.82648375455177));
#206101=CARTESIAN_POINT('Ctrl Pts',(-18.4271451268086,14.9414314869883,
8.6867472734616));
#206102=CARTESIAN_POINT('Ctrl Pts',(-18.4230272925522,14.9705217166792,
8.60375903069658));
#206103=CARTESIAN_POINT('Ctrl Pts',(-18.4189094582958,14.9974622098978,
8.52002479361661));
#206104=CARTESIAN_POINT('Ctrl Pts',(-18.4147916240394,15.0222175337942,
8.43565878066583));
#206105=CARTESIAN_POINT('Ctrl Pts',(-18.4078580498408,15.0639003370249,
8.29360400764394));
#206106=CARTESIAN_POINT('Ctrl Pts',(-18.4009244756422,15.099399552533,8.14970818352137));
#206107=CARTESIAN_POINT('Ctrl Pts',(-18.3939909014436,15.1285731159382,
8.00452425630458));
#206108=CARTESIAN_POINT('Ctrl Pts',(-18.3870586441602,15.1577411383182,
7.85936790432009));
#206109=CARTESIAN_POINT('Ctrl Pts',(-18.3801263868768,15.1805858405798,
7.71292426128421));
#206110=CARTESIAN_POINT('Ctrl Pts',(-18.3731941295934,15.1970161634336,
7.56575695606789));
#206111=CARTESIAN_POINT('Ctrl Pts',(-18.3662616283674,15.2134470644621,
7.41858447210896));
#206112=CARTESIAN_POINT('Ctrl Pts',(-18.3593291271414,15.2234630944089,
7.27068860316925));
#206113=CARTESIAN_POINT('Ctrl Pts',(-18.3523966259154,15.2270249522307,
7.12263915111047));
#206114=CARTESIAN_POINT('Ctrl Pts',(-18.3454645000055,15.2305866172184,
6.97459771424611));
#206115=CARTESIAN_POINT('Ctrl Pts',(-18.3385323740956,15.2276948022499,
6.82640304141277));
#206116=CARTESIAN_POINT('Ctrl Pts',(-18.3316002481857,15.2183623246744,
6.67862601146172));
#206117=CARTESIAN_POINT('Ctrl Pts',(-18.3246665810175,15.2090277721571,
6.53081612541791));
#206118=CARTESIAN_POINT('Ctrl Pts',(-18.3177329138493,15.1932497165721,
6.3834243978359));
#206119=CARTESIAN_POINT('Ctrl Pts',(-18.3107992466811,15.1710929950943,
6.23701830178168));
#206120=CARTESIAN_POINT('Ctrl Pts',(-18.3066814908311,15.1579345946017,
6.15007086922187));
#206121=CARTESIAN_POINT('Ctrl Pts',(-18.3025637349812,15.1425274812018,
6.06347096462066));
#206122=CARTESIAN_POINT('Ctrl Pts',(-18.2984459791312,15.1248938320092,
5.97733609473846));
#206123=CARTESIAN_POINT('Ctrl Pts',(-18.2915124972733,15.0952022739807,
5.83230210549236));
#206124=CARTESIAN_POINT('Ctrl Pts',(-18.2845790154154,15.0591850609188,
5.68853703671448));
#206125=CARTESIAN_POINT('Ctrl Pts',(-18.2776455335575,15.0169755996428,
5.54659597396457));
#206126=CARTESIAN_POINT('Ctrl Pts',(-18.2707133684712,14.9747741545734,
5.40468186794047));
#206127=CARTESIAN_POINT('Ctrl Pts',(-18.263781203385,14.9263829017666,5.26459139352123));
#206128=CARTESIAN_POINT('Ctrl Pts',(-18.2568490382987,14.8719853167288,
5.12686518888486));
#206129=CARTESIAN_POINT('Ctrl Pts',(-18.2499166281586,14.8175858087221,
4.98913411559094));
#206130=CARTESIAN_POINT('Ctrl Pts',(-18.2429842180185,14.7571796619472,
4.85376778802202));
#206131=CARTESIAN_POINT('Ctrl Pts',(-18.2360518078784,14.6909989751094,
4.72128806118977));
#206132=CARTESIAN_POINT('Ctrl Pts',(-18.2291197722066,14.6248218631567,
4.58881549052106));
#206133=CARTESIAN_POINT('Ctrl Pts',(-18.2221877365348,14.552870983883,4.45922950391654));
#206134=CARTESIAN_POINT('Ctrl Pts',(-18.215255700863,14.4754249908955,4.33302850155644));
#206135=CARTESIAN_POINT('Ctrl Pts',(-18.2083221218366,14.3979617552632,
4.20679940169296));
#206136=CARTESIAN_POINT('Ctrl Pts',(-18.2013885428103,14.3150011343056,
4.08395707380847));
#206137=CARTESIAN_POINT('Ctrl Pts',(-18.1944549637839,14.2268661502294,
3.96497254856659));
#206138=CARTESIAN_POINT('Ctrl Pts',(-18.1903367539303,14.1745182418128,
3.89430150805252));
#206139=CARTESIAN_POINT('Ctrl Pts',(-18.1862185440766,14.120345759108,3.82499086876333));
#206140=CARTESIAN_POINT('Ctrl Pts',(-18.182100334223,14.0644233505464,3.75713410309268));
#206141=CARTESIAN_POINT('Ctrl Pts',(-18.1751666150798,13.9702682956653,
3.64288549220289));
#206142=CARTESIAN_POINT('Ctrl Pts',(-18.1682328959365,13.8711179308502,
3.53272057308594));
#206143=CARTESIAN_POINT('Ctrl Pts',(-18.1612991767932,13.7673500985625,
3.42706735854301));
#206144=CARTESIAN_POINT('Ctrl Pts',(-18.154366774106,13.6636019679364,3.32143420362576));
#206145=CARTESIAN_POINT('Ctrl Pts',(-18.1474343714188,13.5552383504529,
3.22031127992502));
#206146=CARTESIAN_POINT('Ctrl Pts',(-18.1405019687316,13.4426745623103,
3.12409038809465));
#206147=CARTESIAN_POINT('Ctrl Pts',(-18.1335693228231,13.3301068249018,
3.02786612038391));
#206148=CARTESIAN_POINT('Ctrl Pts',(-18.1266366769147,13.2133388710388,
2.93654444601232));
#206149=CARTESIAN_POINT('Ctrl Pts',(-18.1197040310062,13.0928201831575,
2.85047779954232));
#206150=CARTESIAN_POINT('Ctrl Pts',(-18.1127717611685,12.972308032975,2.76441582187359));
#206151=CARTESIAN_POINT('Ctrl Pts',(-18.1058394913308,12.8480458254472,
2.68360849304188));
#206152=CARTESIAN_POINT('Ctrl Pts',(-18.0989072214931,12.7205131946589,
2.60836572275157));
#206153=CARTESIAN_POINT('Ctrl Pts',(-18.0919734128154,12.5929522539073,
2.53310624991183));
#206154=CARTESIAN_POINT('Ctrl Pts',(-18.0850396041378,12.4621197240941,
2.46341397180051));
#206155=CARTESIAN_POINT('Ctrl Pts',(-18.0781057954601,12.328521626002,2.39955383811791));
#206156=CARTESIAN_POINT('Ctrl Pts',(-18.0739887600783,12.249196089006,2.36163608727154));
#206157=CARTESIAN_POINT('Ctrl Pts',(-18.0698717246966,12.1688960160921,
2.32577360896849));
#206158=CARTESIAN_POINT('Ctrl Pts',(-18.0657546893148,12.0877310379076,
2.29201399724091));
#206159=CARTESIAN_POINT('Ctrl Pts',(-18.0588213575568,11.9510444008739,
2.23516080886065));
#206160=CARTESIAN_POINT('Ctrl Pts',(-18.0518880257988,11.8118565702988,
2.18425443407282));
#206161=CARTESIAN_POINT('Ctrl Pts',(-18.0449546940409,11.6707017706744,
2.13949610615628));
#206162=CARTESIAN_POINT('Ctrl Pts',(-18.0380226791153,11.52957378027,2.09474627909029));
#206163=CARTESIAN_POINT('Ctrl Pts',(-18.0310906641897,11.3864798811559,
2.05614226907002));
#206164=CARTESIAN_POINT('Ctrl Pts',(-18.0241586492642,11.2419704520384,
2.02383576503533));
#206165=CARTESIAN_POINT('Ctrl Pts',(-18.0172263879248,11.0974558860127,
1.99152811259429));
#206166=CARTESIAN_POINT('Ctrl Pts',(-18.0102941265854,10.9515260112177,
1.96551848947931));
#206167=CARTESIAN_POINT('Ctrl Pts',(-18.0033618652459,10.8047429609757,
1.94590780222078));
#206168=CARTESIAN_POINT('Ctrl Pts',(-17.9964299772503,10.6579678158787,
1.92629817111502));
#206169=CARTESIAN_POINT('Ctrl Pts',(-17.9894980892546,10.5103399151234,
1.9130868291269));
#206170=CARTESIAN_POINT('Ctrl Pts',(-17.9825662012589,10.3624281190368,
1.9063229891009));
#206171=CARTESIAN_POINT('Ctrl Pts',(-17.9756327668903,10.2144833266306,
1.89955764019033));
#206172=CARTESIAN_POINT('Ctrl Pts',(-17.9686993325218,10.0662548427467,
1.89924268229057));
#206173=CARTESIAN_POINT('Ctrl Pts',(-17.9617658981532,9.91831378778123,
1.90537524602953));
#206174=CARTESIAN_POINT('Ctrl Pts',(-17.9576469469043,9.8304263195057,1.90901842338271));
#206175=CARTESIAN_POINT('Ctrl Pts',(-17.9535279956555,9.74264030258537,
1.91493606689122));
#206176=CARTESIAN_POINT('Ctrl Pts',(-17.9494090444066,9.65507506418636,
1.92311887274498));
#206177=CARTESIAN_POINT('Ctrl Pts',(-17.9424753846608,9.50767162774376,
1.93689344499123));
#206178=CARTESIAN_POINT('Ctrl Pts',(-17.9355417249149,9.36084306546452,
1.95709434074805));
#206179=CARTESIAN_POINT('Ctrl Pts',(-17.9286080651691,9.21515569028204,
1.98364918658131));
#206180=CARTESIAN_POINT('Ctrl Pts',(-17.921675723217,9.06949600407137,2.01019898546813));
#206181=CARTESIAN_POINT('Ctrl Pts',(-17.9147433812648,8.9249773972537,2.04310026581364));
#206182=CARTESIAN_POINT('Ctrl Pts',(-17.9078110393127,8.78215725526951,
2.08222931317227));
#206183=CARTESIAN_POINT('Ctrl Pts',(-17.9008784555401,8.63933213129698,
2.12135972546763));
#206184=CARTESIAN_POINT('Ctrl Pts',(-17.8939458717674,8.49820591040426,
2.16671825537547));
#206185=CARTESIAN_POINT('Ctrl Pts',(-17.8870132879947,8.35932258344625,
2.21813081380062));
#206186=CARTESIAN_POINT('Ctrl Pts',(-17.8800810809331,8.22044680329677,
2.26954057850861));
#206187=CARTESIAN_POINT('Ctrl Pts',(-17.8731488738714,8.08381398289625,
2.32700359783838));
#206188=CARTESIAN_POINT('Ctrl Pts',(-17.8662166668098,7.94994985065518,
2.39029695679961));
#206189=CARTESIAN_POINT('Ctrl Pts',(-17.8592829213363,7.81605601096829,
2.45360436197322));
#206190=CARTESIAN_POINT('Ctrl Pts',(-17.8523491758629,7.68493238611156,
2.52274455078309));
#206191=CARTESIAN_POINT('Ctrl Pts',(-17.8454154303894,7.55708231303193,
2.59744753083239));
#206192=CARTESIAN_POINT('Ctrl Pts',(-17.8412980867591,7.48116336186096,
2.64180708228259));
#206193=CARTESIAN_POINT('Ctrl Pts',(-17.8371807431287,7.40639825299786,
2.68812726300884));
#206194=CARTESIAN_POINT('Ctrl Pts',(-17.8330633994984,7.33288794460905,
2.73634405566748));
#206195=CARTESIAN_POINT('Ctrl Pts',(-17.8261558247304,7.20956135421445,
2.81723628382821));
#206196=CARTESIAN_POINT('Ctrl Pts',(-17.8192482499625,7.08972242521831,
2.90349902317069));
#206197=CARTESIAN_POINT('Ctrl Pts',(-17.8123406751945,6.9738347131051,2.9948061723449));
#206198=CARTESIAN_POINT('Ctrl Pts',(-17.805433730195,6.85795756655736,3.08610499698111));
#206199=CARTESIAN_POINT('Ctrl Pts',(-17.7985267851956,6.74603118445736,
3.18244710971482));
#206200=CARTESIAN_POINT('Ctrl Pts',(-17.7916198401962,6.63848738561534,
3.28346506457867));
#206201=CARTESIAN_POINT('Ctrl Pts',(-17.7847137708704,6.53095722135077,
3.38447021222218));
#206202=CARTESIAN_POINT('Ctrl Pts',(-17.7778077015447,6.4278087750554,3.49014978807379));
#206203=CARTESIAN_POINT('Ctrl Pts',(-17.7709016322189,6.32943824184797,
3.60009829050449));
#206204=CARTESIAN_POINT('Ctrl Pts',(-17.763994324437,6.23105006798389,3.71006650985363));
#206205=CARTESIAN_POINT('Ctrl Pts',(-17.757087016655,6.13744174453664,3.82430493647222));
#206206=CARTESIAN_POINT('Ctrl Pts',(-17.7501797088731,6.04897067901331,
3.94237323066272));
#206207=CARTESIAN_POINT('Ctrl Pts',(-17.7447864725821,5.97989233816772,
4.03456113210717));
#206208=CARTESIAN_POINT('Ctrl Pts',(-17.739393236291,5.91394518475807,4.12908318533048));
#206209=CARTESIAN_POINT('Ctrl Pts',(-17.734,5.85128156875001,4.22571665929507));
#206210=CARTESIAN_POINT('',(-17.734,7.81752421401937,2.45527019889639));
#206211=CARTESIAN_POINT('Origin',(-17.734,10.1295,7.));
#206212=CARTESIAN_POINT('',(-18.5963464936225,10.1295586128697,12.0988854733127));
#206213=CARTESIAN_POINT('Ctrl Pts',(-18.5963464895958,10.1295586962519,
12.098655931404));
#206214=CARTESIAN_POINT('Ctrl Pts',(-18.580370831183,10.4708377603055,12.0988021573896));
#206215=CARTESIAN_POINT('Ctrl Pts',(-18.5256132911341,11.6404949371434,
11.9829820272798));
#206216=CARTESIAN_POINT('Ctrl Pts',(-18.4320738694491,13.4987506203882,
11.0980785037433));
#206217=CARTESIAN_POINT('Ctrl Pts',(-18.3157282245409,15.0255448975692,
9.04320498956965));
#206218=CARTESIAN_POINT('Ctrl Pts',(-18.1993825796327,15.4123695196911,
6.51259611415262));
#206219=CARTESIAN_POINT('Ctrl Pts',(-18.0830369347245,14.5690183264701,
4.09545070325184));
#206220=CARTESIAN_POINT('Ctrl Pts',(-17.9666912898164,12.6921474590521,
2.35466759323519));
#206221=CARTESIAN_POINT('Ctrl Pts',(-17.8503456449082,10.2181819306684,
1.69542365644608));
#206222=CARTESIAN_POINT('Ctrl Pts',(-17.772781881636,8.55581177954194,2.07969166083582));
#206223=CARTESIAN_POINT('Ctrl Pts',(-17.734,7.81752421401937,2.45527019889639));
#206224=CARTESIAN_POINT('Ctrl Pts',(-18.8525174996886,5.6491961756188,9.4344770775744));
#206225=CARTESIAN_POINT('Ctrl Pts',(-18.8455851001287,5.71989903564874,
9.56459549072555));
#206226=CARTESIAN_POINT('Ctrl Pts',(-18.8386527005687,5.79627683687807,
9.69163676155592));
#206227=CARTESIAN_POINT('Ctrl Pts',(-18.8317203010087,5.87803557818646,
9.81511123582243));
#206228=CARTESIAN_POINT('Ctrl Pts',(-18.8247881781597,5.95979105604538,
9.93858078153081));
#206229=CARTESIAN_POINT('Ctrl Pts',(-18.8178560553106,6.04692686039238,
10.0584835408014));
#206230=CARTESIAN_POINT('Ctrl Pts',(-18.8109239324616,6.13910564900675,
10.1743588208583));
#206231=CARTESIAN_POINT('Ctrl Pts',(-18.8039903457579,6.23130390299313,
10.2902585702695));
#206232=CARTESIAN_POINT('Ctrl Pts',(-18.7970567590541,6.32854706254942,
10.4021288829091));
#206233=CARTESIAN_POINT('Ctrl Pts',(-18.7901231723504,6.4304571219091,10.5095416774908));
#206234=CARTESIAN_POINT('Ctrl Pts',(-18.7871190496248,6.47461180524522,
10.5560805369597));
#206235=CARTESIAN_POINT('Ctrl Pts',(-18.7841149268993,6.51964208174608,
10.601783054832));
#206236=CARTESIAN_POINT('Ctrl Pts',(-18.7811108041737,6.56551500754935,
10.646616510354));
#206237=CARTESIAN_POINT('Ctrl Pts',(-18.7741773223733,6.6713892095192,10.7500916264889));
#206238=CARTESIAN_POINT('Ctrl Pts',(-18.7672438405729,6.78179109135341,
10.8489706372656));
#206239=CARTESIAN_POINT('Ctrl Pts',(-18.7603103587725,6.8962990704977,10.9428685939891));
#206240=CARTESIAN_POINT('Ctrl Pts',(-18.7533781937436,7.01078530286897,
11.0367487180902));
#206241=CARTESIAN_POINT('Ctrl Pts',(-18.7464460287148,7.12937582121679,
11.1256494659908));
#206242=CARTESIAN_POINT('Ctrl Pts',(-18.739513863686,7.2516156736085,11.2092259150478));
#206243=CARTESIAN_POINT('Ctrl Pts',(-18.7325814536027,7.37385984722273,
11.2928053185622));
#206244=CARTESIAN_POINT('Ctrl Pts',(-18.7256490435193,7.49975334201189,
11.3710598572636));
#206245=CARTESIAN_POINT('Ctrl Pts',(-18.718716633436,7.62881146378363,11.4436874152933));
#206246=CARTESIAN_POINT('Ctrl Pts',(-18.7117845978205,7.75786261422604,
11.516311050202));
#206247=CARTESIAN_POINT('Ctrl Pts',(-18.704852562205,7.8900777610185,11.5833081513277));
#206248=CARTESIAN_POINT('Ctrl Pts',(-18.6979205265895,8.02494679887543,
11.64442211945));
#206249=CARTESIAN_POINT('Ctrl Pts',(-18.6909869476181,8.15984586411983,
11.7055496940518));
#206250=CARTESIAN_POINT('Ctrl Pts',(-18.6840533686468,8.29739969982356,
11.7607913819451));
#206251=CARTESIAN_POINT('Ctrl Pts',(-18.6771197896754,8.43707679425738,
11.8099381173425));
#206252=CARTESIAN_POINT('Ctrl Pts',(-18.6730015795388,8.5200382242095,11.8391288981399));
#206253=CARTESIAN_POINT('Ctrl Pts',(-18.6688833694022,8.60374831456234,
11.8661704298008));
#206254=CARTESIAN_POINT('Ctrl Pts',(-18.6647651592655,8.68809285583543,
11.8910271359655));
#206255=CARTESIAN_POINT('Ctrl Pts',(-18.6577998241514,8.83074900390097,
11.9330685283489));
#206256=CARTESIAN_POINT('Ctrl Pts',(-18.6508344890373,8.97526829574175,
11.9688711530495));
#206257=CARTESIAN_POINT('Ctrl Pts',(-18.6438691539232,9.12109290423389,
11.9982913209625));
#206258=CARTESIAN_POINT('Ctrl Pts',(-18.6369053501428,9.26688545308524,
12.0277050208312));
#206259=CARTESIAN_POINT('Ctrl Pts',(-18.6299415463624,9.41398242822589,
12.0507390002111));
#206260=CARTESIAN_POINT('Ctrl Pts',(-18.622977742582,9.56181530050721,12.0673005715037));
#206261=CARTESIAN_POINT('Ctrl Pts',(-18.6160146854246,9.70963232291145,
12.0838603671502));
#206262=CARTESIAN_POINT('Ctrl Pts',(-18.6090516282673,9.85818476303232,
12.0939491026305));
#206263=CARTESIAN_POINT('Ctrl Pts',(-18.60208857111,10.0068979934788,12.097525845741));
#206264=CARTESIAN_POINT('Ctrl Pts',(-18.6001745459505,10.0477767135858,
12.0985090311648));
#206265=CARTESIAN_POINT('Ctrl Pts',(-18.598260520791,10.0886675622518,12.099000469371));
#206266=CARTESIAN_POINT('Ctrl Pts',(-18.5963464956315,10.1295585712674,
12.0989999996636));
#206267=CARTESIAN_POINT('Origin',(11.,-13.5,22.));
#206268=CARTESIAN_POINT('',(7.,-13.5,16.));
#206269=CARTESIAN_POINT('Origin',(11.,-13.5,16.));
#206270=CARTESIAN_POINT('',(7.,-13.5,22.));
#206271=CARTESIAN_POINT('',(7.,-13.5,22.));
#206272=CARTESIAN_POINT('Origin',(11.,-13.5,22.));
#206273=CARTESIAN_POINT('Origin',(2.22044604925031E-15,2.25,16.));
#206274=CARTESIAN_POINT('Origin',(11.,17.5,22.));
#206275=CARTESIAN_POINT('',(6.55407155365721,16.8045,22.));
#206276=CARTESIAN_POINT('',(9.25758668237251,21.6489752747581,22.));
#206277=CARTESIAN_POINT('Origin',(11.,17.5,22.));
#206278=CARTESIAN_POINT('',(9.25758668237251,21.6489752747581,16.));
#206279=CARTESIAN_POINT('',(9.25758668237251,21.6489752747581,22.));
#206280=CARTESIAN_POINT('',(6.55407155365721,16.8045,16.));
#206281=CARTESIAN_POINT('Origin',(11.,17.5,16.));
#206282=CARTESIAN_POINT('',(6.55407155365721,16.8045,22.));
#206283=CARTESIAN_POINT('Origin',(2.22044604925031E-15,2.25,16.));
#206284=CARTESIAN_POINT('',(9.25758668237251,21.5062266006623,16.));
#206285=CARTESIAN_POINT('',(9.25758668237251,11.8781133003311,16.));
#206286=CARTESIAN_POINT('',(7.0995,19.4175,16.));
#206287=CARTESIAN_POINT('Origin',(10.7505,17.8045,16.));
#206288=CARTESIAN_POINT('',(7.0995,16.8045,16.));
#206289=CARTESIAN_POINT('',(7.0995,9.52725,16.));
#206290=CARTESIAN_POINT('',(-3.54975,16.8045,16.));
#206291=CARTESIAN_POINT('Origin',(-11.,-13.5,22.));
#206292=CARTESIAN_POINT('',(-15.,-13.5,16.));
#206293=CARTESIAN_POINT('Origin',(-11.,-13.5,16.));
#206294=CARTESIAN_POINT('',(-15.,-13.5,22.));
#206295=CARTESIAN_POINT('',(-15.,-13.5,22.));
#206296=CARTESIAN_POINT('Origin',(-11.,-13.5,22.));
#206297=CARTESIAN_POINT('Origin',(2.22044604925031E-15,2.25,16.));
#206298=CARTESIAN_POINT('Origin',(-11.,17.5,22.));
#206299=CARTESIAN_POINT('',(-9.25758668237251,21.6489752747581,22.));
#206300=CARTESIAN_POINT('',(-6.55407155365721,16.8045,22.));
#206301=CARTESIAN_POINT('Origin',(-11.,17.5,22.));
#206302=CARTESIAN_POINT('',(-6.55407155365721,16.8045,16.));
#206303=CARTESIAN_POINT('',(-6.55407155365721,16.8045,22.));
#206304=CARTESIAN_POINT('',(-9.25758668237251,21.6489752747581,16.));
#206305=CARTESIAN_POINT('Origin',(-11.,17.5,16.));
#206306=CARTESIAN_POINT('',(-9.25758668237251,21.6489752747581,22.));
#206307=CARTESIAN_POINT('Origin',(2.22044604925031E-15,2.25,16.));
#206308=CARTESIAN_POINT('',(-7.0995,16.8045,16.));
#206309=CARTESIAN_POINT('',(-7.0995,19.4175,16.));
#206310=CARTESIAN_POINT('',(-7.0995,10.83375,16.));
#206311=CARTESIAN_POINT('',(-9.25758668237251,21.5062266006622,16.));
#206312=CARTESIAN_POINT('Origin',(-10.7505,17.8045,16.));
#206313=CARTESIAN_POINT('',(-9.25758668237251,13.2726133003311,16.));
#206314=CARTESIAN_POINT('',(-3.54975,16.8045,16.));
#206315=CARTESIAN_POINT('Origin',(1.5089639216641E-15,6.00000008940697,
22.));
#206316=CARTESIAN_POINT('',(-5.,6.00000008940697,16.));
#206317=CARTESIAN_POINT('Origin',(1.5089639216641E-15,6.00000008940697,
16.));
#206318=CARTESIAN_POINT('',(-5.,6.00000008940697,22.));
#206319=CARTESIAN_POINT('',(-5.,6.00000008940697,22.));
#206320=CARTESIAN_POINT('Origin',(1.5089639216641E-15,6.00000008940697,
22.));
#206321=CARTESIAN_POINT('Origin',(2.22044604925031E-15,2.25,16.));
#206322=CARTESIAN_POINT('Origin',(7.0995,16.8045,0.));
#206323=CARTESIAN_POINT('',(7.0995,19.4175,0.));
#206324=CARTESIAN_POINT('',(7.0995,19.4175,0.));
#206325=CARTESIAN_POINT('',(7.0995,16.8045,0.));
#206326=CARTESIAN_POINT('',(7.0995,16.8045,0.));
#206327=CARTESIAN_POINT('',(7.0995,16.8045,0.));
#206328=CARTESIAN_POINT('Origin',(-9.25758668237251,24.2952266006623,0.));
#206329=CARTESIAN_POINT('',(-9.25758668237251,21.5062266006623,0.));
#206330=CARTESIAN_POINT('',(-9.25758668237251,21.5062266006623,0.));
#206331=CARTESIAN_POINT('',(-9.25758668237251,24.2952266006623,0.));
#206332=CARTESIAN_POINT('',(-9.25758668237251,21.5062266006623,0.));
#206333=CARTESIAN_POINT('',(-9.25758668237251,24.2952266006623,22.));
#206334=CARTESIAN_POINT('',(-9.25758668237251,24.2952266006623,0.));
#206335=CARTESIAN_POINT('',(-9.25758668237251,21.5062266006623,22.));
#206336=CARTESIAN_POINT('Origin',(-7.0995,16.8045,0.));
#206337=CARTESIAN_POINT('',(-7.0995,16.8045,0.));
#206338=CARTESIAN_POINT('',(7.0995,16.8045,0.));
#206339=CARTESIAN_POINT('',(-7.0995,16.8045,0.));
#206340=CARTESIAN_POINT('',(7.0995,16.8045,22.));
#206341=CARTESIAN_POINT('Origin',(0.,1.05261330033112,22.));
#206342=CARTESIAN_POINT('',(-9.06658668237251,24.4862266006622,22.));
#206343=CARTESIAN_POINT('Origin',(-9.06658668237251,24.2952266006623,22.));
#206344=CARTESIAN_POINT('',(-7.30158668237251,24.4862266006622,22.));
#206345=CARTESIAN_POINT('',(-9.06658668237251,24.4862266006622,22.));
#206346=CARTESIAN_POINT('',(-7.11058668237251,24.6772266006623,22.));
#206347=CARTESIAN_POINT('Origin',(-7.30158668237251,24.6772266006623,22.));
#206348=CARTESIAN_POINT('',(-7.11058668237251,25.8032266006623,22.));
#206349=CARTESIAN_POINT('',(-7.11058668237251,24.6772266006623,22.));
#206350=CARTESIAN_POINT('',(-7.36458668237251,26.0572266006623,22.));
#206351=CARTESIAN_POINT('Origin',(-7.36458668237251,25.8032266006623,22.));
#206352=CARTESIAN_POINT('',(-18.734,24.211,22.));
#206353=CARTESIAN_POINT('',(-7.36458668237251,26.0572266006622,22.));
#206354=CARTESIAN_POINT('',(-23.734,19.211,22.));
#206355=CARTESIAN_POINT('Origin',(-18.734,19.211,22.));
#206356=CARTESIAN_POINT('',(-23.734,6.1295,22.));
#206357=CARTESIAN_POINT('',(-23.734,19.211,22.));
#206358=CARTESIAN_POINT('',(-23.534,6.1295,22.));
#206359=CARTESIAN_POINT('',(-11.867,6.1295,22.));
#206360=CARTESIAN_POINT('',(-23.534,-5.8705,22.));
#206361=CARTESIAN_POINT('',(-23.534,0.591056650165565,22.));
#206362=CARTESIAN_POINT('',(-23.734,-5.8705,22.));
#206363=CARTESIAN_POINT('',(-11.867,-5.8705,22.));
#206364=CARTESIAN_POINT('',(-23.734,-18.952,22.));
#206365=CARTESIAN_POINT('',(-23.734,19.211,22.));
#206366=CARTESIAN_POINT('',(-18.734,-23.952,22.));
#206367=CARTESIAN_POINT('Origin',(-18.734,-18.952,22.));
#206368=CARTESIAN_POINT('',(18.734,-23.952,22.));
#206369=CARTESIAN_POINT('',(-18.734,-23.952,22.));
#206370=CARTESIAN_POINT('',(23.734,-18.952,22.));
#206371=CARTESIAN_POINT('Origin',(18.734,-18.952,22.));
#206372=CARTESIAN_POINT('',(23.734,-5.8705,22.));
#206373=CARTESIAN_POINT('',(23.734,19.211,22.));
#206374=CARTESIAN_POINT('',(23.534,-5.8705,22.));
#206375=CARTESIAN_POINT('',(11.867,-5.8705,22.));
#206376=CARTESIAN_POINT('',(23.534,6.1295,22.));
#206377=CARTESIAN_POINT('',(23.534,0.591056650165565,22.));
#206378=CARTESIAN_POINT('',(23.734,6.1295,22.));
#206379=CARTESIAN_POINT('',(11.867,6.1295,22.));
#206380=CARTESIAN_POINT('',(23.734,19.211,22.));
#206381=CARTESIAN_POINT('',(23.734,19.211,22.));
#206382=CARTESIAN_POINT('',(18.734,24.211,22.));
#206383=CARTESIAN_POINT('Origin',(18.734,19.211,22.));
#206384=CARTESIAN_POINT('',(7.36458668237251,26.0572266006622,22.));
#206385=CARTESIAN_POINT('',(7.36458668237251,26.0572266006622,22.));
#206386=CARTESIAN_POINT('',(7.11058668237251,25.8032266006622,22.));
#206387=CARTESIAN_POINT('Origin',(7.36458668237251,25.8032266006622,22.));
#206388=CARTESIAN_POINT('',(7.11058668237251,24.6772266006623,22.));
#206389=CARTESIAN_POINT('',(7.11058668237251,24.6772266006623,22.));
#206390=CARTESIAN_POINT('',(7.30158668237251,24.4862266006622,22.));
#206391=CARTESIAN_POINT('Origin',(7.30158668237251,24.6772266006623,22.));
#206392=CARTESIAN_POINT('',(9.06658668237251,24.4862266006622,22.));
#206393=CARTESIAN_POINT('',(9.06658668237251,24.4862266006622,22.));
#206394=CARTESIAN_POINT('',(9.25758668237251,24.2952266006623,22.));
#206395=CARTESIAN_POINT('Origin',(9.06658668237251,24.2952266006623,22.));
#206396=CARTESIAN_POINT('',(9.25758668237251,21.5062266006623,22.));
#206397=CARTESIAN_POINT('',(-21.234,0.12950000000008,22.));
#206398=CARTESIAN_POINT('Origin',(-18.734,0.12950000000008,22.));
#206399=CARTESIAN_POINT('',(16.234,0.12950000000008,22.));
#206400=CARTESIAN_POINT('Origin',(18.734,0.12950000000008,22.));
#206401=CARTESIAN_POINT('Ctrl Pts',(-17.1140743056112,17.8480877707428,
22.));
#206402=CARTESIAN_POINT('Ctrl Pts',(-17.0603911270984,17.8998883320905,
22.));
#206403=CARTESIAN_POINT('Ctrl Pts',(-17.0098645090452,17.9545614843891,
22.));
#206404=CARTESIAN_POINT('Ctrl Pts',(-16.9624881824911,18.0117359214698,
22.));
#206405=CARTESIAN_POINT('Ctrl Pts',(-16.913424543523,18.0709466316106,22.));
#206406=CARTESIAN_POINT('Ctrl Pts',(-16.8677390829926,18.1328404012223,
22.));
#206407=CARTESIAN_POINT('Ctrl Pts',(-16.8254531773348,18.1970544302611,
22.));
#206408=CARTESIAN_POINT('Ctrl Pts',(-16.785318687812,18.2580013873046,22.));
#206409=CARTESIAN_POINT('Ctrl Pts',(-16.7482465752263,18.3210394462862,
22.));
#206410=CARTESIAN_POINT('Ctrl Pts',(-16.7142835835435,18.3858911656733,
22.));
#206411=CARTESIAN_POINT('Ctrl Pts',(-16.6991852702862,18.414721122225,22.));
#206412=CARTESIAN_POINT('Ctrl Pts',(-16.6847017945038,18.443909871674,22.));
#206413=CARTESIAN_POINT('Ctrl Pts',(-16.6708392558117,18.4734345779294,
22.));
#206414=CARTESIAN_POINT('Ctrl Pts',(-16.6640109132328,18.4879777156138,
22.));
#206415=CARTESIAN_POINT('Ctrl Pts',(-16.6573332485221,18.5026023792008,
22.));
#206416=CARTESIAN_POINT('Ctrl Pts',(-16.6508071085471,18.5173059065043,
22.));
#206417=CARTESIAN_POINT('Ctrl Pts',(-16.6447949281281,18.53085147238,22.));
#206418=CARTESIAN_POINT('Ctrl Pts',(-16.638910878667,18.5444653615358,22.));
#206419=CARTESIAN_POINT('Ctrl Pts',(-16.6331635636444,18.5581259521741,
22.));
#206420=CARTESIAN_POINT('Ctrl Pts',(-16.6020947551997,18.6319723086221,
22.));
#206421=CARTESIAN_POINT('Ctrl Pts',(-16.5749611536669,18.7073070289838,
22.));
#206422=CARTESIAN_POINT('Ctrl Pts',(-16.5517843887068,18.7837489743025,
22.));
#206423=CARTESIAN_POINT('Ctrl Pts',(-16.5281812491796,18.8615971944571,
22.));
#206424=CARTESIAN_POINT('Ctrl Pts',(-16.5086813563667,18.9405945618219,
22.));
#206425=CARTESIAN_POINT('Ctrl Pts',(-16.4933484509597,19.0203740751758,
22.));
#206426=CARTESIAN_POINT('Ctrl Pts',(-16.47941621323,19.0928656947682,22.));
#206427=CARTESIAN_POINT('Ctrl Pts',(-16.4689246908343,19.1660040425421,
22.));
#206428=CARTESIAN_POINT('Ctrl Pts',(-16.461955492605,19.2395296145576,22.));
#206429=CARTESIAN_POINT('Ctrl Pts',(-16.4592975702873,19.2675708974063,
22.));
#206430=CARTESIAN_POINT('Ctrl Pts',(-16.4571523310073,19.2956686091404,
22.));
#206431=CARTESIAN_POINT('Ctrl Pts',(-16.4555256621827,19.3238086400899,
22.));
#206432=CARTESIAN_POINT('Ctrl Pts',(-16.4546321787531,19.3392651675542,
22.));
#206433=CARTESIAN_POINT('Ctrl Pts',(-16.4538951614737,19.3547344644167,
22.));
#206434=CARTESIAN_POINT('Ctrl Pts',(-16.4533156881431,19.3702141998337,
22.));
#206435=CARTESIAN_POINT('Ctrl Pts',(-16.4528679850542,19.3821738966753,
22.));
#206436=CARTESIAN_POINT('Ctrl Pts',(-16.4525144924858,19.3941365263619,
22.));
#206437=CARTESIAN_POINT('Ctrl Pts',(-16.452255631388,19.4060924704157,22.));
#206438=CARTESIAN_POINT('Ctrl Pts',(-16.4504487968614,19.4895442238956,
22.));
#206439=CARTESIAN_POINT('Ctrl Pts',(-16.4532437926239,19.5727897376045,
22.));
#206440=CARTESIAN_POINT('Ctrl Pts',(-16.4606968610006,19.6554483758565,
22.));
#206441=CARTESIAN_POINT('Ctrl Pts',(-16.4681356985408,19.7379491862843,
22.));
#206442=CARTESIAN_POINT('Ctrl Pts',(-16.4802144629511,19.8198663642554,
22.));
#206443=CARTESIAN_POINT('Ctrl Pts',(-16.4970384375915,19.9008370756969,
22.));
#206444=CARTESIAN_POINT('Ctrl Pts',(-16.5135067566735,19.9800960820144,
22.));
#206445=CARTESIAN_POINT('Ctrl Pts',(-16.5345215459181,20.058449172967,22.));
#206446=CARTESIAN_POINT('Ctrl Pts',(-16.5598157066501,20.135668594405,22.));
#206447=CARTESIAN_POINT('Ctrl Pts',(-16.5701726792028,20.1672869365531,
22.));
#206448=CARTESIAN_POINT('Ctrl Pts',(-16.5812477391057,20.1987151389825,
22.));
#206449=CARTESIAN_POINT('Ctrl Pts',(-16.5930250010084,20.2299370972628,
22.));
#206450=CARTESIAN_POINT('Ctrl Pts',(-16.5995762661519,20.2473047442324,
22.));
#206451=CARTESIAN_POINT('Ctrl Pts',(-16.6063470587533,20.2646137128558,
22.));
#206452=CARTESIAN_POINT('Ctrl Pts',(-16.6133222512795,20.2818311531004,
22.));
#206453=CARTESIAN_POINT('Ctrl Pts',(-16.644281419466,20.3582502091005,22.));
#206454=CARTESIAN_POINT('Ctrl Pts',(-16.6792964912941,20.4329625137279,
22.));
#206455=CARTESIAN_POINT('Ctrl Pts',(-16.7180394494848,20.5057444546796,
22.));
#206456=CARTESIAN_POINT('Ctrl Pts',(-16.7588463546244,20.5824036954548,
22.));
#206457=CARTESIAN_POINT('Ctrl Pts',(-16.8037889572456,20.6569222708542,
22.));
#206458=CARTESIAN_POINT('Ctrl Pts',(-16.8525444691545,20.7290332608009,
22.));
#206459=CARTESIAN_POINT('Ctrl Pts',(-16.9012999810634,20.8011442507476,
22.));
#206460=CARTESIAN_POINT('Ctrl Pts',(-16.9538690009003,20.8708485410036,
22.));
#206461=CARTESIAN_POINT('Ctrl Pts',(-17.0099819921104,20.9378605149736,
22.));
#206462=CARTESIAN_POINT('Ctrl Pts',(-17.0318957015214,20.9640305852723,
22.));
#206463=CARTESIAN_POINT('Ctrl Pts',(-17.0543504354563,20.9897897710343,
22.));
#206464=CARTESIAN_POINT('Ctrl Pts',(-17.0773320398146,21.0151198306805,
22.));
#206465=CARTESIAN_POINT('Ctrl Pts',(-17.08646379095,21.0251847416122,22.));
#206466=CARTESIAN_POINT('Ctrl Pts',(-17.0956794941242,21.0351826951285,
22.));
#206467=CARTESIAN_POINT('Ctrl Pts',(-17.1049759541041,21.045110003522,22.));
#206468=CARTESIAN_POINT('Ctrl Pts',(-17.1654855277221,21.1097256958789,
22.));
#206469=CARTESIAN_POINT('Ctrl Pts',(-17.2292148909451,21.1711403001169,
22.));
#206470=CARTESIAN_POINT('Ctrl Pts',(-17.2958559579295,21.2290794537635,
22.));
#206471=CARTESIAN_POINT('Ctrl Pts',(-17.3510488196552,21.277065295534,22.));
#206472=CARTESIAN_POINT('Ctrl Pts',(-17.4082400388152,21.3226671775257,
22.));
#206473=CARTESIAN_POINT('Ctrl Pts',(-17.4672777521355,21.3657152682276,
22.));
#206474=CARTESIAN_POINT('Ctrl Pts',(-17.4867746843808,21.3799317014277,
22.0000000000001));
#206475=CARTESIAN_POINT('Ctrl Pts',(-17.5064731515178,21.3938694861353,
22.));
#206476=CARTESIAN_POINT('Ctrl Pts',(-17.5263681121617,21.4075220975473,
22.));
#206477=CARTESIAN_POINT('Ctrl Pts',(-17.542293137778,21.4184504019736,22.));
#206478=CARTESIAN_POINT('Ctrl Pts',(-17.55834542777,21.429196741247,22.));
#206479=CARTESIAN_POINT('Ctrl Pts',(-17.5745064519429,21.439747587913,22.));
#206480=CARTESIAN_POINT('Ctrl Pts',(-17.6490342197562,21.4884036039023,
22.0000000000001));
#206481=CARTESIAN_POINT('Ctrl Pts',(-17.7259441256673,21.5329559340006,
22.));
#206482=CARTESIAN_POINT('Ctrl Pts',(-17.8049553049308,21.5731139747841,
22.));
#206483=CARTESIAN_POINT('Ctrl Pts',(-17.8827965257828,21.6126773751883,
22.));
#206484=CARTESIAN_POINT('Ctrl Pts',(-17.9626779315913,21.6479763829434,
22.));
#206485=CARTESIAN_POINT('Ctrl Pts',(-18.0443633906767,21.6786957524571,
22.));
#206486=CARTESIAN_POINT('Ctrl Pts',(-18.0530581575348,21.6819655847986,
22.));
#206487=CARTESIAN_POINT('Ctrl Pts',(-18.0617733892786,21.6851834888842,
22.));
#206488=CARTESIAN_POINT('Ctrl Pts',(-18.0705086704292,21.6883495949495,
22.));
#206489=CARTESIAN_POINT('Ctrl Pts',(-19.3957372685686,21.6839949024184,
22.));
#206490=CARTESIAN_POINT('Ctrl Pts',(-19.477389057327,21.6544306829991,22.));
#206491=CARTESIAN_POINT('Ctrl Pts',(-19.5571491338509,21.6204660242301,
22.));
#206492=CARTESIAN_POINT('Ctrl Pts',(-19.6348154715246,21.5824187572536,
22.));
#206493=CARTESIAN_POINT('Ctrl Pts',(-19.7143271161632,21.5434675093651,
22.));
#206494=CARTESIAN_POINT('Ctrl Pts',(-19.7916450683047,21.5002366972975,
22.));
#206495=CARTESIAN_POINT('Ctrl Pts',(-19.8665231149463,21.4530209100354,
22.));
#206496=CARTESIAN_POINT('Ctrl Pts',(-19.9365885412779,21.4088398127381,
22.));
#206497=CARTESIAN_POINT('Ctrl Pts',(-20.0045177600369,21.3611685582522,
22.));
#206498=CARTESIAN_POINT('Ctrl Pts',(-20.0700782126376,21.3102210028104,
22.));
#206499=CARTESIAN_POINT('Ctrl Pts',(-20.0997466183463,21.2871654459197,
22.));
#206500=CARTESIAN_POINT('Ctrl Pts',(-20.1289294820831,21.2634386377592,
22.));
#206501=CARTESIAN_POINT('Ctrl Pts',(-20.1576028623549,21.2390591151444,
22.));
#206502=CARTESIAN_POINT('Ctrl Pts',(-20.1753080822265,21.2240052636568,
22.));
#206503=CARTESIAN_POINT('Ctrl Pts',(-20.1928190152043,21.2087025308569,
22.));
#206504=CARTESIAN_POINT('Ctrl Pts',(-20.2101297112266,21.1931551680194,
22.));
#206505=CARTESIAN_POINT('Ctrl Pts',(-20.222291744835,21.182232005305,22.));
#206506=CARTESIAN_POINT('Ctrl Pts',(-20.2343567146449,21.1711862914419,
22.));
#206507=CARTESIAN_POINT('Ctrl Pts',(-20.2463056588354,21.1600355900683,
22.));
#206508=CARTESIAN_POINT('Ctrl Pts',(-20.3097374358009,21.1008413389894,
22.));
#206509=CARTESIAN_POINT('Ctrl Pts',(-20.3700068738241,21.038599740636,22.));
#206510=CARTESIAN_POINT('Ctrl Pts',(-20.426883413529,20.9735889911137,22.));
#206511=CARTESIAN_POINT('Ctrl Pts',(-20.4830375565956,20.9094039519309,
22.));
#206512=CARTESIAN_POINT('Ctrl Pts',(-20.535884892703,20.8425188203227,22.));
#206513=CARTESIAN_POINT('Ctrl Pts',(-20.5851610183447,20.7731751876268,
22.));
#206514=CARTESIAN_POINT('Ctrl Pts',(-20.6305982452024,20.7092338300444,
22.));
#206515=CARTESIAN_POINT('Ctrl Pts',(-20.6729988898147,20.6432013951179,
22.));
#206516=CARTESIAN_POINT('Ctrl Pts',(-20.7121179614365,20.5752560755747,
22.));
#206517=CARTESIAN_POINT('Ctrl Pts',(-20.7284900120376,20.5468197103046,
22.0000000000001));
#206518=CARTESIAN_POINT('Ctrl Pts',(-20.7442868026563,20.5180482040854,
22.));
#206519=CARTESIAN_POINT('Ctrl Pts',(-20.7594882606863,20.4889543859677,
22.));
#206520=CARTESIAN_POINT('Ctrl Pts',(-20.769344952432,20.4700898272965,22.));
#206521=CARTESIAN_POINT('Ctrl Pts',(-20.7789513234994,20.4510897578356,
22.));
#206522=CARTESIAN_POINT('Ctrl Pts',(-20.7883016018661,20.4319576715327,
22.));
#206523=CARTESIAN_POINT('Ctrl Pts',(-20.7942275528717,20.4198322778685,
22.));
#206524=CARTESIAN_POINT('Ctrl Pts',(-20.800046810587,20.4076616313445,22.));
#206525=CARTESIAN_POINT('Ctrl Pts',(-20.8057567064001,20.3954502940177,
22.));
#206526=CARTESIAN_POINT('Ctrl Pts',(-20.8408822399145,20.3203298798152,
22.));
#206527=CARTESIAN_POINT('Ctrl Pts',(-20.8718943362061,20.2436277257691,
22.));
#206528=CARTESIAN_POINT('Ctrl Pts',(-20.898546197771,20.1655724028405,22.));
#206529=CARTESIAN_POINT('Ctrl Pts',(-20.9251980593358,20.0875170799122,
22.));
#206530=CARTESIAN_POINT('Ctrl Pts',(-20.9474901582818,20.008107858314,22.));
#206531=CARTESIAN_POINT('Ctrl Pts',(-20.9651213884777,19.9275640466204,
22.));
#206532=CARTESIAN_POINT('Ctrl Pts',(-20.982945860616,19.8461374580334,22.));
#206533=CARTESIAN_POINT('Ctrl Pts',(-20.9960059981342,19.7635500467728,
22.));
#206534=CARTESIAN_POINT('Ctrl Pts',(-21.0043774598022,19.6801932612386,
22.));
#206535=CARTESIAN_POINT('Ctrl Pts',(-21.0078359299807,19.6457563888755,
22.));
#206536=CARTESIAN_POINT('Ctrl Pts',(-21.0104935728588,19.6111883610475,
22.));
#206537=CARTESIAN_POINT('Ctrl Pts',(-21.0123533015418,19.5765177064329,
22.));
#206538=CARTESIAN_POINT('Ctrl Pts',(-21.01308526083,19.5628718945969,22.));
#206539=CARTESIAN_POINT('Ctrl Pts',(-21.0136936024307,19.5492081941022,
22.));
#206540=CARTESIAN_POINT('Ctrl Pts',(-21.0141780332164,19.535546001816,22.));
#206541=CARTESIAN_POINT('Ctrl Pts',(-21.0170628012175,19.4541881354373,
22.));
#206542=CARTESIAN_POINT('Ctrl Pts',(-21.0155662532645,19.372753622897,22.));
#206543=CARTESIAN_POINT('Ctrl Pts',(-21.009821014486,19.2915996489842,22.));
#206544=CARTESIAN_POINT('Ctrl Pts',(-21.0040551149971,19.2101538336328,
22.));
#206545=CARTESIAN_POINT('Ctrl Pts',(-20.9940095377668,19.1289895605332,
22.));
#206546=CARTESIAN_POINT('Ctrl Pts',(-20.9797676620055,19.0484794558067,
22.));
#206547=CARTESIAN_POINT('Ctrl Pts',(-20.9656474978483,18.9686573934531,
22.));
#206548=CARTESIAN_POINT('Ctrl Pts',(-20.9474020142679,18.8894774430081,
22.));
#206549=CARTESIAN_POINT('Ctrl Pts',(-20.9250689442011,18.8113285395616,
22.));
#206550=CARTESIAN_POINT('Ctrl Pts',(-20.915771730189,18.7787953017227,22.));
#206551=CARTESIAN_POINT('Ctrl Pts',(-20.9057656352848,18.7464411369984,
22.));
#206552=CARTESIAN_POINT('Ctrl Pts',(-20.8950513997073,18.714296014732,22.));
#206553=CARTESIAN_POINT('Ctrl Pts',(-20.8895107302012,18.6976727570651,
22.));
#206554=CARTESIAN_POINT('Ctrl Pts',(-20.8837798036466,18.681103370745,22.));
#206555=CARTESIAN_POINT('Ctrl Pts',(-20.8778666056241,18.6646133670345,
22.));
#206556=CARTESIAN_POINT('Ctrl Pts',(-20.8511334433403,18.5900631923957,
22.));
#206557=CARTESIAN_POINT('Ctrl Pts',(-20.8206474037361,18.5170371727757,
22.));
#206558=CARTESIAN_POINT('Ctrl Pts',(-20.7864673395051,18.4458945668894,
22.));
#206559=CARTESIAN_POINT('Ctrl Pts',(-20.7601551393027,18.3911281838788,
22.));
#206560=CARTESIAN_POINT('Ctrl Pts',(-20.7316529155262,18.3374783045939,
21.9999999999999));
#206561=CARTESIAN_POINT('Ctrl Pts',(-20.7009723139099,18.2851235072403,
22.));
#206562=CARTESIAN_POINT('Ctrl Pts',(-20.6917380438118,18.2693657217269,
22.));
#206563=CARTESIAN_POINT('Ctrl Pts',(-20.6823063515041,18.2537253600017,
22.));
#206564=CARTESIAN_POINT('Ctrl Pts',(-20.6726773431573,18.2382075723836,
22.));
#206565=CARTESIAN_POINT('Ctrl Pts',(-20.6644524248536,18.2249525692911,
21.9999999999999));
#206566=CARTESIAN_POINT('Ctrl Pts',(-20.6560858067932,18.2117907655657,
22.));
#206567=CARTESIAN_POINT('Ctrl Pts',(-20.6475820990968,18.1987316736659,
22.));
#206568=CARTESIAN_POINT('Ctrl Pts',(-20.6064305731469,18.1355355269517,
22.));
#206569=CARTESIAN_POINT('Ctrl Pts',(-20.5620419258381,18.0746943297043,
22.));
#206570=CARTESIAN_POINT('Ctrl Pts',(-20.5144495325811,18.0165478115783,
22.));
#206571=CARTESIAN_POINT('Ctrl Pts',(-20.4703173158397,17.9626288013104,
22.));
#206572=CARTESIAN_POINT('Ctrl Pts',(-20.4234297243619,17.9110267653547,
22.));
#206573=CARTESIAN_POINT('Ctrl Pts',(-20.3737908005412,17.8620457668345,
22.));
#206574=CARTESIAN_POINT('Ctrl Pts',(-20.368202240041,17.8565312783541,22.));
#206575=CARTESIAN_POINT('Ctrl Pts',(-20.3625787852046,17.8510500502091,
22.));
#206576=CARTESIAN_POINT('Ctrl Pts',(-20.3569208045551,17.8456022314362,
21.9999999999999));
#206577=CARTESIAN_POINT('Ctrl Pts',(20.3539256943888,17.8480877707428,22.));
#206578=CARTESIAN_POINT('Ctrl Pts',(20.4076088569716,17.8998883167192,22.));
#206579=CARTESIAN_POINT('Ctrl Pts',(20.4581354582059,17.954561454772,22.));
#206580=CARTESIAN_POINT('Ctrl Pts',(20.5055117676561,18.011735878447,22.));
#206581=CARTESIAN_POINT('Ctrl Pts',(20.5545753925315,18.0709465790738,22.));
#206582=CARTESIAN_POINT('Ctrl Pts',(20.6002608381634,18.1328403404668,22.));
#206583=CARTESIAN_POINT('Ctrl Pts',(20.6425467287697,18.1970543621783,22.));
#206584=CARTESIAN_POINT('Ctrl Pts',(20.6826812143694,18.2580013280037,22.));
#206585=CARTESIAN_POINT('Ctrl Pts',(20.7197533213128,18.321039397649,22.));
#206586=CARTESIAN_POINT('Ctrl Pts',(20.7537163061537,18.3858911290265,22.));
#206587=CARTESIAN_POINT('Ctrl Pts',(20.7688146169019,18.4147210919254,22.));
#206588=CARTESIAN_POINT('Ctrl Pts',(20.7832980898944,18.4439098480094,22.));
#206589=CARTESIAN_POINT('Ctrl Pts',(20.79716062556,18.4734345611379,22.));
#206590=CARTESIAN_POINT('Ctrl Pts',(20.8039889483082,18.4879776631471,22.));
#206591=CARTESIAN_POINT('Ctrl Pts',(20.8106665939401,18.5026022906791,22.));
#206592=CARTESIAN_POINT('Ctrl Pts',(20.8171927156004,18.5173057815627,22.));
#206593=CARTESIAN_POINT('Ctrl Pts',(20.8232049158819,18.5308513966511,22.));
#206594=CARTESIAN_POINT('Ctrl Pts',(20.8290889843231,18.5444653356248,22.));
#206595=CARTESIAN_POINT('Ctrl Pts',(20.834836317356,18.5581259764514,22.));
#206596=CARTESIAN_POINT('Ctrl Pts',(20.8659051086395,18.6319723320065,22.));
#206597=CARTESIAN_POINT('Ctrl Pts',(20.8930386939032,18.7073070517053,22.));
#206598=CARTESIAN_POINT('Ctrl Pts',(20.9162154441631,18.7837489961396,22.));
#206599=CARTESIAN_POINT('Ctrl Pts',(20.939818572744,18.8615972286665,22.));
#206600=CARTESIAN_POINT('Ctrl Pts',(20.9593184548383,18.9405946085653,22.));
#206601=CARTESIAN_POINT('Ctrl Pts',(20.9746513504446,19.0203741339557,22.));
#206602=CARTESIAN_POINT('Ctrl Pts',(20.9885835808428,19.0928657726744,22.));
#206603=CARTESIAN_POINT('Ctrl Pts',(20.9990750958871,19.1660041393111,22.));
#206604=CARTESIAN_POINT('Ctrl Pts',(21.0060442872368,19.2395297293499,22.));
#206605=CARTESIAN_POINT('Ctrl Pts',(21.0087022058165,19.2675710073175,22.));
#206606=CARTESIAN_POINT('Ctrl Pts',(21.0108474418568,19.2956687140012,22.));
#206607=CARTESIAN_POINT('Ctrl Pts',(21.0124741079748,19.3238087397167,22.));
#206608=CARTESIAN_POINT('Ctrl Pts',(21.0133675811686,19.3392651129519,22.));
#206609=CARTESIAN_POINT('Ctrl Pts',(21.0141045914371,19.3547342552799,22.));
#206610=CARTESIAN_POINT('Ctrl Pts',(21.0146840610199,19.370213835923,22.));
#206611=CARTESIAN_POINT('Ctrl Pts',(21.0151317606382,19.3821733978234,22.));
#206612=CARTESIAN_POINT('Ctrl Pts',(21.0154852519447,19.3941358929903,22.));
#206613=CARTESIAN_POINT('Ctrl Pts',(21.0157441139737,19.4060917025175,22.));
#206614=CARTESIAN_POINT('Ctrl Pts',(21.0175509756949,19.4895434728017,22.));
#206615=CARTESIAN_POINT('Ctrl Pts',(21.0147560087132,19.5727890030198,22.));
#206616=CARTESIAN_POINT('Ctrl Pts',(21.0073029715582,19.655447656657,22.));
#206617=CARTESIAN_POINT('Ctrl Pts',(20.9998641358153,19.737948808113,22.));
#206618=CARTESIAN_POINT('Ctrl Pts',(20.987785339035,19.819866321382,22.));
#206619=CARTESIAN_POINT('Ctrl Pts',(20.9709612973755,19.9008373573407,22.));
#206620=CARTESIAN_POINT('Ctrl Pts',(20.9545235681866,19.9799491420218,22.));
#206621=CARTESIAN_POINT('Ctrl Pts',(20.933556230191,20.0581583683546,22.));
#206622=CARTESIAN_POINT('Ctrl Pts',(20.9083249440286,20.1352385562694,22.));
#206623=CARTESIAN_POINT('Ctrl Pts',(20.8979275365846,20.1670020626737,22.));
#206624=CARTESIAN_POINT('Ctrl Pts',(20.886805437583,20.198573773065,22.));
#206625=CARTESIAN_POINT('Ctrl Pts',(20.8749747526326,20.2299373637517,22.));
#206626=CARTESIAN_POINT('Ctrl Pts',(20.8684234889834,20.2473050100404,22.));
#206627=CARTESIAN_POINT('Ctrl Pts',(20.8616526979763,20.2646139778576,22.));
#206628=CARTESIAN_POINT('Ctrl Pts',(20.854677507136,20.2818314171768,22.));
#206629=CARTESIAN_POINT('Ctrl Pts',(20.8237183426601,20.3582504783803,22.));
#206630=CARTESIAN_POINT('Ctrl Pts',(20.7887032753635,20.4329627854486,22.));
#206631=CARTESIAN_POINT('Ctrl Pts',(20.7499603220884,20.505744726553,22.));
#206632=CARTESIAN_POINT('Ctrl Pts',(20.7091534306779,20.5824039514245,22.));
#206633=CARTESIAN_POINT('Ctrl Pts',(20.6642108439443,20.6569225092783,22.));
#206634=CARTESIAN_POINT('Ctrl Pts',(20.6154553493761,20.7290334807154,22.));
#206635=CARTESIAN_POINT('Ctrl Pts',(20.5666998548079,20.8011444521524,22.));
#206636=CARTESIAN_POINT('Ctrl Pts',(20.5141308537666,20.8708487229331,22.));
#206637=CARTESIAN_POINT('Ctrl Pts',(20.4580178821339,20.9378606771181,22.));
#206638=CARTESIAN_POINT('Ctrl Pts',(20.4361041795504,20.9640307406671,22.));
#206639=CARTESIAN_POINT('Ctrl Pts',(20.4136494525221,20.9897899196015,22.));
#206640=CARTESIAN_POINT('Ctrl Pts',(20.3906678551117,21.0151199723788,22.));
#206641=CARTESIAN_POINT('Ctrl Pts',(20.3815361086865,21.0251848784325,22.));
#206642=CARTESIAN_POINT('Ctrl Pts',(20.3723204102617,21.0351828270963,22.));
#206643=CARTESIAN_POINT('Ctrl Pts',(20.3630239550768,21.0451101306559,22.));
#206644=CARTESIAN_POINT('Ctrl Pts',(20.3025143985113,21.1097258066671,22.));
#206645=CARTESIAN_POINT('Ctrl Pts',(20.2387850522983,21.1711403943428,22.));
#206646=CARTESIAN_POINT('Ctrl Pts',(20.1721440016478,21.2290795318308,22.));
#206647=CARTESIAN_POINT('Ctrl Pts',(20.11695115458,21.2770653592361,22.));
#206648=CARTESIAN_POINT('Ctrl Pts',(20.0597599496963,21.3226672272365,22.));
#206649=CARTESIAN_POINT('Ctrl Pts',(20.0007222499054,21.3657153046774,22.));
#206650=CARTESIAN_POINT('Ctrl Pts',(19.9812253064434,21.3799317449347,22.));
#206651=CARTESIAN_POINT('Ctrl Pts',(19.9615268276842,21.3938695363309,22.));
#206652=CARTESIAN_POINT('Ctrl Pts',(19.9416318550109,21.4075221540601,22.));
#206653=CARTESIAN_POINT('Ctrl Pts',(19.9257068576964,21.4184504375137,22.));
#206654=CARTESIAN_POINT('Ctrl Pts',(19.9096545963614,21.4291967564363,22.));
#206655=CARTESIAN_POINT('Ctrl Pts',(19.8934936011196,21.4397475834371,22.));
#206656=CARTESIAN_POINT('Ctrl Pts',(19.8189658486552,21.4884035858209,22.));
#206657=CARTESIAN_POINT('Ctrl Pts',(19.7420559565434,21.5329559037425,22.));
#206658=CARTESIAN_POINT('Ctrl Pts',(19.6630447888977,21.5731139344032,22.));
#206659=CARTESIAN_POINT('Ctrl Pts',(19.5852035756509,21.6126773267864,22.));
#206660=CARTESIAN_POINT('Ctrl Pts',(19.5053221751299,21.6479763280926,22.));
#206661=CARTESIAN_POINT('Ctrl Pts',(19.423636718432,21.6786956932901,22.));
#206662=CARTESIAN_POINT('Ctrl Pts',(19.414941951073,21.6819655254561,22.));
#206663=CARTESIAN_POINT('Ctrl Pts',(19.4062267187917,21.6851834293815,22.));
#206664=CARTESIAN_POINT('Ctrl Pts',(19.3974914370684,21.688349535301,22.));
#206665=CARTESIAN_POINT('Ctrl Pts',(18.0722627314313,21.6839949024184,22.));
#206666=CARTESIAN_POINT('Ctrl Pts',(17.9906108868453,21.6544306627852,22.));
#206667=CARTESIAN_POINT('Ctrl Pts',(17.910850754587,21.6204659928942,22.));
#206668=CARTESIAN_POINT('Ctrl Pts',(17.8331843622586,21.5824187212756,22.));
#206669=CARTESIAN_POINT('Ctrl Pts',(17.7536727057626,21.5434674902368,22.));
#206670=CARTESIAN_POINT('Ctrl Pts',(17.6763547404621,21.5002367065575,22.));
#206671=CARTESIAN_POINT('Ctrl Pts',(17.601476680063,21.4530209559562,22.));
#206672=CARTESIAN_POINT('Ctrl Pts',(17.53141126819,21.4088399101981,22.));
#206673=CARTESIAN_POINT('Ctrl Pts',(17.463482061701,21.3611687172218,22.));
#206674=CARTESIAN_POINT('Ctrl Pts',(17.3979216194972,21.3102212303572,22.));
#206675=CARTESIAN_POINT('Ctrl Pts',(17.3682532365539,21.287165718535,22.));
#206676=CARTESIAN_POINT('Ctrl Pts',(17.3390703946074,21.2634389577077,22.));
#206677=CARTESIAN_POINT('Ctrl Pts',(17.3103970351346,21.2390594843875,22.));
#206678=CARTESIAN_POINT('Ctrl Pts',(17.2926918259638,21.2240056615169,22.));
#206679=CARTESIAN_POINT('Ctrl Pts',(17.2751809033557,21.2087029580218,22.));
#206680=CARTESIAN_POINT('Ctrl Pts',(17.2578702173692,21.1931556251064,22.));
#206681=CARTESIAN_POINT('Ctrl Pts',(17.2457081795529,21.1822324733025,22.));
#206682=CARTESIAN_POINT('Ctrl Pts',(17.2336432055526,21.1711867704329,22.));
#206683=CARTESIAN_POINT('Ctrl Pts',(17.2216942572027,21.160036080102,22.));
#206684=CARTESIAN_POINT('Ctrl Pts',(17.1582624698647,21.1008418985699,22.));
#206685=CARTESIAN_POINT('Ctrl Pts',(17.0979930211184,21.0386003723497,22.));
#206686=CARTESIAN_POINT('Ctrl Pts',(17.0411164708952,20.973589694329,22.));
#206687=CARTESIAN_POINT('Ctrl Pts',(16.9849623314314,20.9094047417274,22.));
#206688=CARTESIAN_POINT('Ctrl Pts',(16.9321149974797,20.8425196974351,22.));
#206689=CARTESIAN_POINT('Ctrl Pts',(16.8828388728811,20.7731761494878,22.));
#206690=CARTESIAN_POINT('Ctrl Pts',(16.8374016308483,20.7092348473427,22.));
#206691=CARTESIAN_POINT('Ctrl Pts',(16.7950009722696,20.6432024641904,22.));
#206692=CARTESIAN_POINT('Ctrl Pts',(16.7558818883965,20.5752571902803,22.));
#206693=CARTESIAN_POINT('Ctrl Pts',(16.7395098281522,20.5468208362648,22.));
#206694=CARTESIAN_POINT('Ctrl Pts',(16.7237130285085,20.5180493400384,22.));
#206695=CARTESIAN_POINT('Ctrl Pts',(16.7085115621276,20.4889555304732,22.));
#206696=CARTESIAN_POINT('Ctrl Pts',(16.6986548604459,20.4700909686944,22.));
#206697=CARTESIAN_POINT('Ctrl Pts',(16.6890484799558,20.4510908953963,22.));
#206698=CARTESIAN_POINT('Ctrl Pts',(16.6796981927033,20.4319588044811,22.));
#206699=CARTESIAN_POINT('Ctrl Pts',(16.6737722459446,20.4198334281067,22.));
#206700=CARTESIAN_POINT('Ctrl Pts',(16.6679529923645,20.4076627987652,22.));
#206701=CARTESIAN_POINT('Ctrl Pts',(16.6622431005404,20.3954514784257,22.));
#206702=CARTESIAN_POINT('Ctrl Pts',(16.6271175635218,20.3203311087503,22.));
#206703=CARTESIAN_POINT('Ctrl Pts',(16.5961054651676,20.2436289901797,22.));
#206704=CARTESIAN_POINT('Ctrl Pts',(16.5694536034806,20.1655736906577,22.));
#206705=CARTESIAN_POINT('Ctrl Pts',(16.5428017417936,20.087518391136,22.));
#206706=CARTESIAN_POINT('Ctrl Pts',(16.5205096446651,20.0081091808815,22.));
#206707=CARTESIAN_POINT('Ctrl Pts',(16.5028784187468,19.9275653652902,22.));
#206708=CARTESIAN_POINT('Ctrl Pts',(16.4850539498385,19.8461387677624,22.));
#206709=CARTESIAN_POINT('Ctrl Pts',(16.4719938186516,19.7635513318282,22.));
#206710=CARTESIAN_POINT('Ctrl Pts',(16.4636223658545,19.6801945089039,22.));
#206711=CARTESIAN_POINT('Ctrl Pts',(16.4601638998612,19.6457576262764,22.));
#206712=CARTESIAN_POINT('Ctrl Pts',(16.457506261361,19.6111895860526,22.));
#206713=CARTESIAN_POINT('Ctrl Pts',(16.4556465372103,19.5765189171097,22.));
#206714=CARTESIAN_POINT('Ctrl Pts',(16.4549145796191,19.5628730980147,22.));
#206715=CARTESIAN_POINT('Ctrl Pts',(16.4543062397689,19.5492093899537,22.));
#206716=CARTESIAN_POINT('Ctrl Pts',(16.4538218107824,19.535547189819,22.));
#206717=CARTESIAN_POINT('Ctrl Pts',(16.450937053514,19.4541892772202,22.));
#206718=CARTESIAN_POINT('Ctrl Pts',(16.4524336138896,19.3727547084355,22.));
#206719=CARTESIAN_POINT('Ctrl Pts',(16.4581788662374,19.291600671179,22.));
#206720=CARTESIAN_POINT('Ctrl Pts',(16.4639447791349,19.2101547952154,22.));
#206721=CARTESIAN_POINT('Ctrl Pts',(16.4739903706192,19.1289904543258,22.));
#206722=CARTESIAN_POINT('Ctrl Pts',(16.4882322609474,19.048480277483,22.));
#206723=CARTESIAN_POINT('Ctrl Pts',(16.5023524377413,18.9686581538369,22.));
#206724=CARTESIAN_POINT('Ctrl Pts',(16.5205979332128,18.8894781376779,22.));
#206725=CARTESIAN_POINT('Ctrl Pts',(16.5429310139029,18.8113291667476,22.));
#206726=CARTESIAN_POINT('Ctrl Pts',(16.5522282344977,18.7787958932563,22.));
#206727=CARTESIAN_POINT('Ctrl Pts',(16.5622343360937,18.7464416926568,21.9999999999999));
#206728=CARTESIAN_POINT('Ctrl Pts',(16.5729485784318,18.7142965345088,22.));
#206729=CARTESIAN_POINT('Ctrl Pts',(16.5784892537261,18.6976732514091,22.));
#206730=CARTESIAN_POINT('Ctrl Pts',(16.5842201862524,18.6811038396758,22.));
#206731=CARTESIAN_POINT('Ctrl Pts',(16.5901333904085,18.6646138106646,22.));
#206732=CARTESIAN_POINT('Ctrl Pts',(16.6168665610553,18.5900635756494,22.));
#206733=CARTESIAN_POINT('Ctrl Pts',(16.6473526068873,18.5170374956828,22.));
#206734=CARTESIAN_POINT('Ctrl Pts',(16.6815326747322,18.4458948319454,22.));
#206735=CARTESIAN_POINT('Ctrl Pts',(16.7078448953081,18.3911283677854,22.));
#206736=CARTESIAN_POINT('Ctrl Pts',(16.7363471408355,18.3374784103201,22.));
#206737=CARTESIAN_POINT('Ctrl Pts',(16.7670277653193,18.2851235392682,22.));
#206738=CARTESIAN_POINT('Ctrl Pts',(16.7762620345021,18.2693657448798,22.));
#206739=CARTESIAN_POINT('Ctrl Pts',(16.7856937256623,18.2537253744878,22.));
#206740=CARTESIAN_POINT('Ctrl Pts',(16.7953227326228,18.2382075784408,22.));
#206741=CARTESIAN_POINT('Ctrl Pts',(16.8035476401832,18.2249525835537,22.));
#206742=CARTESIAN_POINT('Ctrl Pts',(16.8119142470167,18.2117907879613,22.));
#206743=CARTESIAN_POINT('Ctrl Pts',(16.8204179429878,18.198731704156,22.));
#206744=CARTESIAN_POINT('Ctrl Pts',(16.8615694556779,18.1355355298381,22.));
#206745=CARTESIAN_POINT('Ctrl Pts',(16.9059580849723,18.0746943089278,21.9999999999999));
#206746=CARTESIAN_POINT('Ctrl Pts',(16.9535504550158,18.0165477730384,22.));
#206747=CARTESIAN_POINT('Ctrl Pts',(16.9976827241167,17.9626286560282,22.));
#206748=CARTESIAN_POINT('Ctrl Pts',(17.0445703727031,17.9110265261487,22.));
#206749=CARTESIAN_POINT('Ctrl Pts',(17.0942093579555,17.8620454496849,22.));
#206750=CARTESIAN_POINT('Ctrl Pts',(17.0997979190133,17.8565309587036,22.));
#206751=CARTESIAN_POINT('Ctrl Pts',(17.1054213743828,17.8510497281848,22.));
#206752=CARTESIAN_POINT('Ctrl Pts',(17.1110793555412,17.8456019071633,22.));
#206753=CARTESIAN_POINT('Ctrl Pts',(20.3539256943887,-20.3149122292573,
22.));
#206754=CARTESIAN_POINT('Ctrl Pts',(20.408139566195,-20.2625995855167,22.));
#206755=CARTESIAN_POINT('Ctrl Pts',(20.4591341972937,-20.2073573541925,
22.));
#206756=CARTESIAN_POINT('Ctrl Pts',(20.5069159265706,-20.1495677196682,
22.));
#206757=CARTESIAN_POINT('Ctrl Pts',(20.5546976558475,-20.091778085144,22.));
#206758=CARTESIAN_POINT('Ctrl Pts',(20.5992668013762,-20.0314403792713,
22.));
#206759=CARTESIAN_POINT('Ctrl Pts',(20.6406036312651,-19.9688911346062,
22.));
#206760=CARTESIAN_POINT('Ctrl Pts',(20.6814854208042,-19.9070304388754,
22.));
#206761=CARTESIAN_POINT('Ctrl Pts',(20.7192059247084,-19.8430059080155,
22.));
#206762=CARTESIAN_POINT('Ctrl Pts',(20.7537163516506,-19.7771088559497,
22.));
#206763=CARTESIAN_POINT('Ctrl Pts',(20.7688146634378,-19.748278895671,22.));
#206764=CARTESIAN_POINT('Ctrl Pts',(20.7832981375853,-19.7190901423257,
22.));
#206765=CARTESIAN_POINT('Ctrl Pts',(20.7971606745034,-19.6895654320343,
22.));
#206766=CARTESIAN_POINT('Ctrl Pts',(20.8039890054239,-19.6750223153312,
22.));
#206767=CARTESIAN_POINT('Ctrl Pts',(20.8106666589183,-19.660397672949,22.));
#206768=CARTESIAN_POINT('Ctrl Pts',(20.8171927881263,-19.6456941670648,
22.));
#206769=CARTESIAN_POINT('Ctrl Pts',(20.8232049803476,-19.6321485719831,
22.));
#206770=CARTESIAN_POINT('Ctrl Pts',(20.8290890410869,-19.618534653263,22.));
#206771=CARTESIAN_POINT('Ctrl Pts',(20.8348363668121,-19.6048740328408,
22.));
#206772=CARTESIAN_POINT('Ctrl Pts',(20.8661434568434,-19.5304612896112,
22.));
#206773=CARTESIAN_POINT('Ctrl Pts',(20.8934547915536,-19.4545373140852,
21.9999999999999));
#206774=CARTESIAN_POINT('Ctrl Pts',(20.916748098317,-19.3774919314298,22.));
#206775=CARTESIAN_POINT('Ctrl Pts',(20.9400414050804,-19.3004465487744,
22.));
#206776=CARTESIAN_POINT('Ctrl Pts',(20.9593170648394,-19.2222788660794,
21.9999999999999));
#206777=CARTESIAN_POINT('Ctrl Pts',(20.9745132363111,-19.1433443390627,
21.9999999999999));
#206778=CARTESIAN_POINT('Ctrl Pts',(20.9885143247977,-19.0706175144489,
21.9999999999999));
#206779=CARTESIAN_POINT('Ctrl Pts',(20.9990521599664,-18.9972388060651,
22.));
#206780=CARTESIAN_POINT('Ctrl Pts',(21.0060443782249,-18.923470317406,22.));
#206781=CARTESIAN_POINT('Ctrl Pts',(21.0087022983456,-18.8954290373673,
22.));
#206782=CARTESIAN_POINT('Ctrl Pts',(21.010847535719,-18.8673313285427,22.));
#206783=CARTESIAN_POINT('Ctrl Pts',(21.012474202948,-18.8391913006101,22.));
#206784=CARTESIAN_POINT('Ctrl Pts',(21.0133676804257,-18.8237348626051,
22.));
#206785=CARTESIAN_POINT('Ctrl Pts',(21.0141046936245,-18.8082656553794,
22.));
#206786=CARTESIAN_POINT('Ctrl Pts',(21.0146841647679,-18.7927860097385,
22.));
#206787=CARTESIAN_POINT('Ctrl Pts',(21.0151318658524,-18.7808263906625,
22.));
#206788=CARTESIAN_POINT('Ctrl Pts',(21.01548535769,-18.768863838497,22.));
#206789=CARTESIAN_POINT('Ctrl Pts',(21.0157442193216,-18.7569079719692,
22.));
#206790=CARTESIAN_POINT('Ctrl Pts',(21.017551069503,-18.6734562086591,22.));
#206791=CARTESIAN_POINT('Ctrl Pts',(21.0147560903276,-18.5902106853063,
22.));
#206792=CARTESIAN_POINT('Ctrl Pts',(21.0073030399704,-18.5075520380821,
22.));
#206793=CARTESIAN_POINT('Ctrl Pts',(20.9998642034238,-18.4250510302545,
22.));
#206794=CARTESIAN_POINT('Ctrl Pts',(20.9877854202568,-18.3431336582205,
22.));
#206795=CARTESIAN_POINT('Ctrl Pts',(20.9709614068361,-18.2621627589815,
22.));
#206796=CARTESIAN_POINT('Ctrl Pts',(20.9545236784523,-18.1830509789684,
22.));
#206797=CARTESIAN_POINT('Ctrl Pts',(20.9335563404747,-18.104841755941,22.));
#206798=CARTESIAN_POINT('Ctrl Pts',(20.9083250537327,-18.0277615701596,
22.));
#206799=CARTESIAN_POINT('Ctrl Pts',(20.8979276440165,-17.9959980584227,
22.));
#206800=CARTESIAN_POINT('Ctrl Pts',(20.8868055423579,-17.9644263425748,
22.));
#206801=CARTESIAN_POINT('Ctrl Pts',(20.874974854388,-17.9330627463293,22.));
#206802=CARTESIAN_POINT('Ctrl Pts',(20.8684235902148,-17.9156951000059,
22.));
#206803=CARTESIAN_POINT('Ctrl Pts',(20.8616527986486,-17.8983861321004,
22.));
#206804=CARTESIAN_POINT('Ctrl Pts',(20.854677607217,-17.8811686926409,22.));
#206805=CARTESIAN_POINT('Ctrl Pts',(20.8226256793881,-17.8020522795121,
22.));
#206806=CARTESIAN_POINT('Ctrl Pts',(20.7862268153504,-17.724765227739,22.));
#206807=CARTESIAN_POINT('Ctrl Pts',(20.7458439642001,-17.6495556859564,
22.));
#206808=CARTESIAN_POINT('Ctrl Pts',(20.7054483430734,-17.5743223612055,
22.));
#206809=CARTESIAN_POINT('Ctrl Pts',(20.6610656710241,-17.501167065488,22.));
#206810=CARTESIAN_POINT('Ctrl Pts',(20.6130013967575,-17.4303438070485,
22.));
#206811=CARTESIAN_POINT('Ctrl Pts',(20.5649371224908,-17.359520548609,22.));
#206812=CARTESIAN_POINT('Ctrl Pts',(20.5131906957729,-17.2910285130232,
22.));
#206813=CARTESIAN_POINT('Ctrl Pts',(20.4580179345364,-17.2251393904043,
22.));
#206814=CARTESIAN_POINT('Ctrl Pts',(20.4361042290218,-17.1989693239199,
22.));
#206815=CARTESIAN_POINT('Ctrl Pts',(20.4136494990236,-17.1732101420222,
22.));
#206816=CARTESIAN_POINT('Ctrl Pts',(20.3906678986206,-17.1478800862692,
22.));
#206817=CARTESIAN_POINT('Ctrl Pts',(20.3815361507949,-17.1378151788001,
22.));
#206818=CARTESIAN_POINT('Ctrl Pts',(20.3723204509639,-17.1278172287239,
22.));
#206819=CARTESIAN_POINT('Ctrl Pts',(20.3630239943621,-17.1178899237497,
22.));
#206820=CARTESIAN_POINT('Ctrl Pts',(20.3025144308281,-17.0532742409372,
22.));
#206821=CARTESIAN_POINT('Ctrl Pts',(20.2387850776619,-16.9918596463669,
22.));
#206822=CARTESIAN_POINT('Ctrl Pts',(20.1721440203357,-16.933920502147,22.));
#206823=CARTESIAN_POINT('Ctrl Pts',(20.1169511671352,-16.8859346686413,
22.));
#206824=CARTESIAN_POINT('Ctrl Pts',(20.0597599562651,-16.8403327947037,
22.));
#206825=CARTESIAN_POINT('Ctrl Pts',(20.0007222507865,-16.7972847116374,
22.));
#206826=CARTESIAN_POINT('Ctrl Pts',(19.9812253134723,-16.7830682753746,
22.));
#206827=CARTESIAN_POINT('Ctrl Pts',(19.9615268410592,-16.7691304877775,
22.));
#206828=CARTESIAN_POINT('Ctrl Pts',(19.94163187493,-16.7554778736493,22.));
#206829=CARTESIAN_POINT('Ctrl Pts',(19.9257068621322,-16.7445495788584,
22.));
#206830=CARTESIAN_POINT('Ctrl Pts',(19.9096545851051,-16.733803248942,22.));
#206831=CARTESIAN_POINT('Ctrl Pts',(19.8934935740057,-16.7232524113246,
22.));
#206832=CARTESIAN_POINT('Ctrl Pts',(19.818965815021,-16.6745964034672,22.));
#206833=CARTESIAN_POINT('Ctrl Pts',(19.7420559170314,-16.6300440806761,
22.));
#206834=CARTESIAN_POINT('Ctrl Pts',(19.6630447444112,-16.5898860460099,
22.));
#206835=CARTESIAN_POINT('Ctrl Pts',(19.585203529837,-16.5503226514967,22.));
#206836=CARTESIAN_POINT('Ctrl Pts',(19.5053221290521,-16.5150236485074,
22.));
#206837=CARTESIAN_POINT('Ctrl Pts',(19.4236366733768,-16.4843042822826,
22.));
#206838=CARTESIAN_POINT('Ctrl Pts',(19.4149419062245,-16.481034450044,22.));
#206839=CARTESIAN_POINT('Ctrl Pts',(19.4062266741651,-16.4778165460524,
22.));
#206840=CARTESIAN_POINT('Ctrl Pts',(19.3974913926779,-16.4746504400725,
22.));
#206841=CARTESIAN_POINT('Ctrl Pts',(18.0722627314314,-16.4790050975816,
22.));
#206842=CARTESIAN_POINT('Ctrl Pts',(17.9909906838445,-16.5084318215279,
22.));
#206843=CARTESIAN_POINT('Ctrl Pts',(17.9115928093154,-16.5422181704993,
22.));
#206844=CARTESIAN_POINT('Ctrl Pts',(17.8342682750801,-16.580050621616,22.));
#206845=CARTESIAN_POINT('Ctrl Pts',(17.7547379110741,-16.6189623155344,
22.));
#206846=CARTESIAN_POINT('Ctrl Pts',(17.6774001286651,-16.6621548599535,
22.));
#206847=CARTESIAN_POINT('Ctrl Pts',(17.6025009734493,-16.7093334978469,
22.));
#206848=CARTESIAN_POINT('Ctrl Pts',(17.5320732406115,-16.7536956070808,
22.));
#206849=CARTESIAN_POINT('Ctrl Pts',(17.463801490032,-16.8015830463496,22.));
#206850=CARTESIAN_POINT('Ctrl Pts',(17.3979216159377,-16.8527787647009,
22.));
#206851=CARTESIAN_POINT('Ctrl Pts',(17.368253233471,-16.875834275562,22.));
#206852=CARTESIAN_POINT('Ctrl Pts',(17.3390703919806,-16.89956103538,22.));
#206853=CARTESIAN_POINT('Ctrl Pts',(17.3103970329429,-16.9239405076492,
22.));
#206854=CARTESIAN_POINT('Ctrl Pts',(17.2926918239748,-16.938994329927,22.));
#206855=CARTESIAN_POINT('Ctrl Pts',(17.2751809015629,-16.9542970328152,
22.));
#206856=CARTESIAN_POINT('Ctrl Pts',(17.257870215766,-16.9698443651112,22.));
#206857=CARTESIAN_POINT('Ctrl Pts',(17.2457081778958,-16.9807675166481,
22.));
#206858=CARTESIAN_POINT('Ctrl Pts',(17.2336432038411,-16.9918132192483,
22.));
#206859=CARTESIAN_POINT('Ctrl Pts',(17.2216942554371,-17.0029639093079,
22.));
#206860=CARTESIAN_POINT('Ctrl Pts',(17.1582584279828,-17.0621618593448,
22.));
#206861=CARTESIAN_POINT('Ctrl Pts',(17.0979853415003,-17.1244075418476,
22.));
#206862=CARTESIAN_POINT('Ctrl Pts',(17.0411056012962,-17.1894227118676,
22.));
#206863=CARTESIAN_POINT('Ctrl Pts',(16.9845622276698,-17.2540534052679,
22.));
#206864=CARTESIAN_POINT('Ctrl Pts',(16.9313716722725,-17.3214217543552,
22.));
#206865=CARTESIAN_POINT('Ctrl Pts',(16.8818040512577,-17.3912811757792,
22.));
#206866=CARTESIAN_POINT('Ctrl Pts',(16.8334273399218,-17.4594621575398,
22.));
#206867=CARTESIAN_POINT('Ctrl Pts',(16.7885012591782,-17.530016710817,22.));
#206868=CARTESIAN_POINT('Ctrl Pts',(16.7473243285968,-17.6027294194584,
22.));
#206869=CARTESIAN_POINT('Ctrl Pts',(16.7339893719953,-17.626277090458,22.0000000000001));
#206870=CARTESIAN_POINT('Ctrl Pts',(16.7210480077412,-17.6500511631493,
22.));
#206871=CARTESIAN_POINT('Ctrl Pts',(16.7085115583106,-17.6740444448892,
22.));
#206872=CARTESIAN_POINT('Ctrl Pts',(16.6986548564673,-17.6929090066348,
22.));
#206873=CARTESIAN_POINT('Ctrl Pts',(16.6890484758239,-17.7119090799142,
22.));
#206874=CARTESIAN_POINT('Ctrl Pts',(16.679698188427,-17.7310411708259,22.));
#206875=CARTESIAN_POINT('Ctrl Pts',(16.6737722417175,-17.7431665469103,
22.));
#206876=CARTESIAN_POINT('Ctrl Pts',(16.6679529881854,-17.7553371759649,
22.));
#206877=CARTESIAN_POINT('Ctrl Pts',(16.6622430964078,-17.7675484960222,
22.));
#206878=CARTESIAN_POINT('Ctrl Pts',(16.6271175593077,-17.8426688647472,
22.));
#206879=CARTESIAN_POINT('Ctrl Pts',(16.5961054609041,-17.9193709825623,
22.));
#206880=CARTESIAN_POINT('Ctrl Pts',(16.5694535992104,-17.9974262815892,
22.));
#206881=CARTESIAN_POINT('Ctrl Pts',(16.5428017375166,-18.0754815806163,
22.));
#206882=CARTESIAN_POINT('Ctrl Pts',(16.5205096404242,-18.1548907906356,
22.));
#206883=CARTESIAN_POINT('Ctrl Pts',(16.502878414596,-18.2354346063206,22.));
#206884=CARTESIAN_POINT('Ctrl Pts',(16.4850539457493,-18.3168612040769,
22.));
#206885=CARTESIAN_POINT('Ctrl Pts',(16.4719938146952,-18.3994486405796,
22.));
#206886=CARTESIAN_POINT('Ctrl Pts',(16.4636223620895,-18.4828054643466,
22.));
#206887=CARTESIAN_POINT('Ctrl Pts',(16.4601638961884,-18.5172423471919,
22.));
#206888=CARTESIAN_POINT('Ctrl Pts',(16.4575062577843,-18.5518103876793,
22.));
#206889=CARTESIAN_POINT('Ctrl Pts',(16.455646533733,-18.5864810569274,22.));
#206890=CARTESIAN_POINT('Ctrl Pts',(16.4549145761463,-18.6001268767863,
22.));
#206891=CARTESIAN_POINT('Ctrl Pts',(16.4543062363129,-18.6137905856188,
22.));
#206892=CARTESIAN_POINT('Ctrl Pts',(16.4538218073552,-18.6274527865309,
22.));
#206893=CARTESIAN_POINT('Ctrl Pts',(16.4509320250045,-18.7089524294447,
22.));
#206894=CARTESIAN_POINT('Ctrl Pts',(16.4524388232547,-18.790528997647,22.));
#206895=CARTESIAN_POINT('Ctrl Pts',(16.4582089280278,-18.8718234286523,
22.));
#206896=CARTESIAN_POINT('Ctrl Pts',(16.46400738077,-18.9535172513681,22.));
#206897=CARTESIAN_POINT('Ctrl Pts',(16.4741115013859,-19.0349271916877,
22.));
#206898=CARTESIAN_POINT('Ctrl Pts',(16.4884372996282,-19.115677127894,22.));
#206899=CARTESIAN_POINT('Ctrl Pts',(16.5025241469637,-19.1950801743737,
22.));
#206900=CARTESIAN_POINT('Ctrl Pts',(16.5206935045672,-19.2738459260412,
22.));
#206901=CARTESIAN_POINT('Ctrl Pts',(16.5429083125862,-19.351591380106,22.));
#206902=CARTESIAN_POINT('Ctrl Pts',(16.5522119455795,-19.3841514261301,
22.));
#206903=CARTESIAN_POINT('Ctrl Pts',(16.5622256149131,-19.4165321317305,
22.));
#206904=CARTESIAN_POINT('Ctrl Pts',(16.5729485780652,-19.4487034546206,
22.));
#206905=CARTESIAN_POINT('Ctrl Pts',(16.578489253474,-19.4653267382297,22.));
#206906=CARTESIAN_POINT('Ctrl Pts',(16.5842201861179,-19.481896150472,22.));
#206907=CARTESIAN_POINT('Ctrl Pts',(16.5901333903942,-19.4983861799902,
22.));
#206908=CARTESIAN_POINT('Ctrl Pts',(16.6168665612538,-19.5729364163756,
22.));
#206909=CARTESIAN_POINT('Ctrl Pts',(16.6473526072598,-19.6459624977086,
22.));
#206910=CARTESIAN_POINT('Ctrl Pts',(16.6815326752298,-19.7171051627546,
22.));
#206911=CARTESIAN_POINT('Ctrl Pts',(16.7078448962084,-19.7718716285596,
22.));
#206912=CARTESIAN_POINT('Ctrl Pts',(16.7363471421602,-19.8255215876092,
22.));
#206913=CARTESIAN_POINT('Ctrl Pts',(16.7670277670848,-19.8778764601534,
22.));
#206914=CARTESIAN_POINT('Ctrl Pts',(16.7762620361372,-19.8936342545421,
22.));
#206915=CARTESIAN_POINT('Ctrl Pts',(16.7856937271573,-19.9092746249327,
22.));
#206916=CARTESIAN_POINT('Ctrl Pts',(16.7953227339677,-19.9247924209762,
22.));
#206917=CARTESIAN_POINT('Ctrl Pts',(16.8035476416632,-19.9380474162847,
21.9999999999999));
#206918=CARTESIAN_POINT('Ctrl Pts',(16.8119142486341,-19.9512092122917,
22.));
#206919=CARTESIAN_POINT('Ctrl Pts',(16.8204179447442,-19.9642682965029,
22.));
#206920=CARTESIAN_POINT('Ctrl Pts',(16.8615694572081,-20.0274644714053,
22.));
#206921=CARTESIAN_POINT('Ctrl Pts',(16.905958086176,-20.0883056928112,21.9999999999999));
#206922=CARTESIAN_POINT('Ctrl Pts',(16.9535504557832,-20.1464522290649,
22.));
#206923=CARTESIAN_POINT('Ctrl Pts',(16.9976827257099,-20.2003713479159,
22.));
#206924=CARTESIAN_POINT('Ctrl Pts',(17.0445703751811,-20.251973479394,22.));
#206925=CARTESIAN_POINT('Ctrl Pts',(17.0942093613684,-20.3009545571532,
22.));
#206926=CARTESIAN_POINT('Ctrl Pts',(17.0997979224383,-20.3064690481884,
22.));
#206927=CARTESIAN_POINT('Ctrl Pts',(17.1054213778192,-20.3119502787582,
22.));
#206928=CARTESIAN_POINT('Ctrl Pts',(17.1110793589886,-20.3173980998282,
22.));
#206929=CARTESIAN_POINT('Ctrl Pts',(-17.1140743056112,-20.3149122292573,
22.));
#206930=CARTESIAN_POINT('Ctrl Pts',(-17.0603910881415,-20.2631116303188,
22.));
#206931=CARTESIAN_POINT('Ctrl Pts',(-17.0098644290427,-20.2084384430962,
22.));
#206932=CARTESIAN_POINT('Ctrl Pts',(-16.9624880608117,-20.1512639730764,
22.));
#206933=CARTESIAN_POINT('Ctrl Pts',(-16.9134243877974,-20.0920532398234,
22.));
#206934=CARTESIAN_POINT('Ctrl Pts',(-16.8677388912856,-20.0301594502243,
22.));
#206935=CARTESIAN_POINT('Ctrl Pts',(-16.8254529492875,-19.9659454033464,
22.));
#206936=CARTESIAN_POINT('Ctrl Pts',(-16.7853184507886,-19.9049984681181,
22.));
#206937=CARTESIAN_POINT('Ctrl Pts',(-16.7482463250095,-19.8419604355437,
22.));
#206938=CARTESIAN_POINT('Ctrl Pts',(-16.71428331717,-19.777108745806,22.));
#206939=CARTESIAN_POINT('Ctrl Pts',(-16.6991849978544,-19.7482788045816,
22.));
#206940=CARTESIAN_POINT('Ctrl Pts',(-16.6847015153359,-19.7190900711551,
22.));
#206941=CARTESIAN_POINT('Ctrl Pts',(-16.6708389693358,-19.6895653814969,
22.));
#206942=CARTESIAN_POINT('Ctrl Pts',(-16.6640105788719,-19.6750221576682,
22.));
#206943=CARTESIAN_POINT('Ctrl Pts',(-16.6573328680918,-19.6603974070189,
22.));
#206944=CARTESIAN_POINT('Ctrl Pts',(-16.6508066838924,-19.6456937917726,
22.));
#206945=CARTESIAN_POINT('Ctrl Pts',(-16.6447945515434,-19.6321483449743,
22.));
#206946=CARTESIAN_POINT('Ctrl Pts',(-16.6389105480172,-19.6185345763601,
22.));
#206947=CARTESIAN_POINT('Ctrl Pts',(-16.6331632765825,-19.6048741071589,
22.));
#206948=CARTESIAN_POINT('Ctrl Pts',(-16.6018561398417,-19.530461373728,
22.));
#206949=CARTESIAN_POINT('Ctrl Pts',(-16.5745447598008,-19.4545374092054,
22.));
#206950=CARTESIAN_POINT('Ctrl Pts',(-16.5512514111518,-19.3774920371772,
22.));
#206951=CARTESIAN_POINT('Ctrl Pts',(-16.5279580625028,-19.3004466651491,
22.));
#206952=CARTESIAN_POINT('Ctrl Pts',(-16.5086823642981,-19.2222789927081,
22.));
#206953=CARTESIAN_POINT('Ctrl Pts',(-16.4934861598923,-19.1433444740215,
22.));
#206954=CARTESIAN_POINT('Ctrl Pts',(-16.4781825851218,-19.0638522352736,
22.));
#206955=CARTESIAN_POINT('Ctrl Pts',(-16.4670158957966,-18.9835813665496,
22.));
#206956=CARTESIAN_POINT('Ctrl Pts',(-16.4600957863878,-18.90287356738,22.));
#206957=CARTESIAN_POINT('Ctrl Pts',(-16.4582781144994,-18.8816744375601,
22.));
#206958=CARTESIAN_POINT('Ctrl Pts',(-16.4567536954935,-18.8604450906499,
22.));
#206959=CARTESIAN_POINT('Ctrl Pts',(-16.4555251072067,-18.8391916010845,
22.));
#206960=CARTESIAN_POINT('Ctrl Pts',(-16.4546315989448,-18.8237346992684,
22.));
#206961=CARTESIAN_POINT('Ctrl Pts',(-16.45389456466,-18.8082650273129,22.));
#206962=CARTESIAN_POINT('Ctrl Pts',(-16.4533150822428,-18.7927849162226,
22.));
#206963=CARTESIAN_POINT('Ctrl Pts',(-16.4528673708036,-18.7808248936061,
22.));
#206964=CARTESIAN_POINT('Ctrl Pts',(-16.4525138752178,-18.7688619391664,
22.));
#206965=CARTESIAN_POINT('Ctrl Pts',(-16.4522550163972,-18.7569056703414,
22.));
#206966=CARTESIAN_POINT('Ctrl Pts',(-16.4504482477209,-18.6734539573408,
22.));
#206967=CARTESIAN_POINT('Ctrl Pts',(-16.4532433131771,-18.5902084834056,
22.));
#206968=CARTESIAN_POINT('Ctrl Pts',(-16.4606964571555,-18.5075498822213,
22.));
#206969=CARTESIAN_POINT('Ctrl Pts',(-16.4681352990784,-18.4250498970387,
22.));
#206970=CARTESIAN_POINT('Ctrl Pts',(-16.4802139851741,-18.3431335304585,
22.));
#206971=CARTESIAN_POINT('Ctrl Pts',(-16.4970377976341,-18.2621636043343,
22.));
#206972=CARTESIAN_POINT('Ctrl Pts',(-16.5135061122501,-18.1829046241824,
22.));
#206973=CARTESIAN_POINT('Ctrl Pts',(-16.5345209017836,-18.104551551424,
22.));
#206974=CARTESIAN_POINT('Ctrl Pts',(-16.5598150664328,-18.0273321413391,
22.));
#206975=CARTESIAN_POINT('Ctrl Pts',(-16.5701720519776,-17.9957137690736,
22.));
#206976=CARTESIAN_POINT('Ctrl Pts',(-16.5812471270599,-17.964285535797,
22.));
#206977=CARTESIAN_POINT('Ctrl Pts',(-16.5930244062011,-17.9330635460661,
22.));
#206978=CARTESIAN_POINT('Ctrl Pts',(-16.5995756745648,-17.9156958984863,
22.));
#206979=CARTESIAN_POINT('Ctrl Pts',(-16.606346470602,-17.8983869289424,
22.));
#206980=CARTESIAN_POINT('Ctrl Pts',(-16.613321666761,-17.8811694874779,
22.));
#206981=CARTESIAN_POINT('Ctrl Pts',(-16.6442808434086,-17.804750444978,
22.));
#206982=CARTESIAN_POINT('Ctrl Pts',(-16.6792959255798,-17.7300381471314,
22.));
#206983=CARTESIAN_POINT('Ctrl Pts',(-16.7180388949535,-17.6572562073792,
22.));
#206984=CARTESIAN_POINT('Ctrl Pts',(-16.7588458333273,-17.5805969275614,
22.));
#206985=CARTESIAN_POINT('Ctrl Pts',(-16.8037884744597,-17.506078309178,
22.));
#206986=CARTESIAN_POINT('Ctrl Pts',(-16.852544028446,-17.4339672739468,
22.));
#206987=CARTESIAN_POINT('Ctrl Pts',(-16.9012995824323,-17.3618562387157,
22.));
#206988=CARTESIAN_POINT('Ctrl Pts',(-16.9538686479157,-17.2921519008718,
22.));
#206989=CARTESIAN_POINT('Ctrl Pts',(-17.0099816867116,-17.2251398785991,
22.));
#206990=CARTESIAN_POINT('Ctrl Pts',(-17.0318954130067,-17.1989697914665,
22.));
#206991=CARTESIAN_POINT('Ctrl Pts',(-17.0543501640382,-17.1732105886975,
22.));
#206992=CARTESIAN_POINT('Ctrl Pts',(-17.0773317856131,-17.1478805119615,
22.));
#206993=CARTESIAN_POINT('Ctrl Pts',(-17.0864635488618,-17.1378155884281,
22.));
#206994=CARTESIAN_POINT('Ctrl Pts',(-17.095679264258,-17.127817622382,22.));
#206995=CARTESIAN_POINT('Ctrl Pts',(-17.1049757365821,-17.1178903015161,
22.));
#206996=CARTESIAN_POINT('Ctrl Pts',(-17.165485351815,-17.0532745693386,
22.));
#206997=CARTESIAN_POINT('Ctrl Pts',(-17.2292147565865,-16.9918599247989,
22.));
#206998=CARTESIAN_POINT('Ctrl Pts',(-17.2958558635168,-16.9339207318737,
22.));
#206999=CARTESIAN_POINT('Ctrl Pts',(-17.3510487599443,-16.8859348561654,
22.));
#207000=CARTESIAN_POINT('Ctrl Pts',(-17.4082400128264,-16.8403329410748,
22.));
#207001=CARTESIAN_POINT('Ctrl Pts',(-17.4672777580112,-16.797284818969,
22.));
#207002=CARTESIAN_POINT('Ctrl Pts',(-17.4896865553589,-16.7809451596297,
22.));
#207003=CARTESIAN_POINT('Ctrl Pts',(-17.5123617016702,-16.7649735008075,
22.));
#207004=CARTESIAN_POINT('Ctrl Pts',(-17.5352952134256,-16.7493800153535,
22.));
#207005=CARTESIAN_POINT('Ctrl Pts',(-17.5482870635507,-16.7405462951581,
22.));
#207006=CARTESIAN_POINT('Ctrl Pts',(-17.561360861439,-16.7318346842869,
22.));
#207007=CARTESIAN_POINT('Ctrl Pts',(-17.5745065855726,-16.7232523975405,
22.));
#207008=CARTESIAN_POINT('Ctrl Pts',(-17.6490343908001,-16.674596348734,
22.));
#207009=CARTESIAN_POINT('Ctrl Pts',(-17.7259443303904,-16.6300439893023,
22.));
#207010=CARTESIAN_POINT('Ctrl Pts',(-17.8049555380687,-16.5898859241834,
22.));
#207011=CARTESIAN_POINT('Ctrl Pts',(-17.8827967752858,-16.5503225057146,
22.));
#207012=CARTESIAN_POINT('Ctrl Pts',(-17.962678191744,-16.51502348347,22.));
#207013=CARTESIAN_POINT('Ctrl Pts',(-18.0443636543755,-16.484304104371,
22.));
#207014=CARTESIAN_POINT('Ctrl Pts',(-18.0530584200154,-16.4810342716093,
22.));
#207015=CARTESIAN_POINT('Ctrl Pts',(-18.0617736504531,-16.47781636714,22.));
#207016=CARTESIAN_POINT('Ctrl Pts',(-18.0705089302109,-16.4746502607264,
22.));
#207017=CARTESIAN_POINT('Ctrl Pts',(-19.3957372685685,-16.4790050975816,
22.));
#207018=CARTESIAN_POINT('Ctrl Pts',(-19.4773890957418,-16.5085693309101,
22.));
#207019=CARTESIAN_POINT('Ctrl Pts',(-19.5571492106159,-16.5425339973348,
22.));
#207020=CARTESIAN_POINT('Ctrl Pts',(-19.6348155858967,-16.5805812675104,
22.));
#207021=CARTESIAN_POINT('Ctrl Pts',(-19.7143272388332,-16.6195325038781,
22.));
#207022=CARTESIAN_POINT('Ctrl Pts',(-19.7916452001604,-16.6627632965025,
22.));
#207023=CARTESIAN_POINT('Ctrl Pts',(-19.8665232563899,-16.7099790586442,
22.));
#207024=CARTESIAN_POINT('Ctrl Pts',(-19.936588672608,-16.754160120401,22.));
#207025=CARTESIAN_POINT('Ctrl Pts',(-20.0045178827681,-16.8018313324713,
22.));
#207026=CARTESIAN_POINT('Ctrl Pts',(-20.0700783280693,-16.8527788406207,
22.));
#207027=CARTESIAN_POINT('Ctrl Pts',(-20.0997467181299,-16.8758343665167,
22.));
#207028=CARTESIAN_POINT('Ctrl Pts',(-20.1289295668893,-16.8995611421252,
22.));
#207029=CARTESIAN_POINT('Ctrl Pts',(-20.1576029328649,-16.9239406308391,
22.));
#207030=CARTESIAN_POINT('Ctrl Pts',(-20.1753081453826,-16.9389944626467,
22.));
#207031=CARTESIAN_POINT('Ctrl Pts',(-20.1928190712341,-16.9542971752936,
22.));
#207032=CARTESIAN_POINT('Ctrl Pts',(-20.2101297603596,-16.9698445175537,
22.));
#207033=CARTESIAN_POINT('Ctrl Pts',(-20.2222917967556,-16.9807676726665,
22.));
#207034=CARTESIAN_POINT('Ctrl Pts',(-20.2343567693431,-16.9918133788689,
22.));
#207035=CARTESIAN_POINT('Ctrl Pts',(-20.2463057162916,-17.002964072546,
22.));
#207036=CARTESIAN_POINT('Ctrl Pts',(-20.3097375002003,-17.0621582755838,
22.));
#207037=CARTESIAN_POINT('Ctrl Pts',(-20.3700069454281,-17.1243998240974,
22.));
#207038=CARTESIAN_POINT('Ctrl Pts',(-20.4268834922198,-17.1894105241983,
22.));
#207039=CARTESIAN_POINT('Ctrl Pts',(-20.4830376328431,-17.2535955037972,
22.));
#207040=CARTESIAN_POINT('Ctrl Pts',(-20.5358849675036,-17.3204805753177,
22.));
#207041=CARTESIAN_POINT('Ctrl Pts',(-20.5851610924645,-17.3898241496929,
22.));
#207042=CARTESIAN_POINT('Ctrl Pts',(-20.6305983299647,-17.4537654693584,
22.0000000000001));
#207043=CARTESIAN_POINT('Ctrl Pts',(-20.6729989843666,-17.5197978689047,
22.));
#207044=CARTESIAN_POINT('Ctrl Pts',(-20.7121180645734,-17.5877431573068,
22.));
#207045=CARTESIAN_POINT('Ctrl Pts',(-20.7391058385126,-17.6346177789475,
22.));
#207046=CARTESIAN_POINT('Ctrl Pts',(-20.7645310103452,-17.6824030516845,
22.));
#207047=CARTESIAN_POINT('Ctrl Pts',(-20.788301742955,-17.7310415486134,
22.0000000000001));
#207048=CARTESIAN_POINT('Ctrl Pts',(-20.7942276911041,-17.7431669305097,
22.0000000000001));
#207049=CARTESIAN_POINT('Ctrl Pts',(-20.8000469460378,-17.755337565341,
22.));
#207050=CARTESIAN_POINT('Ctrl Pts',(-20.8057568391674,-17.7675488911101,
22.));
#207051=CARTESIAN_POINT('Ctrl Pts',(-20.8408823751017,-17.8426692746921,
22.));
#207052=CARTESIAN_POINT('Ctrl Pts',(-20.8718944728201,-17.9193714043448,
22.));
#207053=CARTESIAN_POINT('Ctrl Pts',(-20.8985463344755,-17.9974267111826,
22.));
#207054=CARTESIAN_POINT('Ctrl Pts',(-20.9251981961308,-18.0754820180205,
22.));
#207055=CARTESIAN_POINT('Ctrl Pts',(-20.9474902938315,-18.1548912318264,
22.));
#207056=CARTESIAN_POINT('Ctrl Pts',(-20.9651215210881,-18.2354350462128,
22.));
#207057=CARTESIAN_POINT('Ctrl Pts',(-20.9829459910005,-18.3168616409281,
22.));
#207058=CARTESIAN_POINT('Ctrl Pts',(-20.9960061241615,-18.3994490691394,
22.));
#207059=CARTESIAN_POINT('Ctrl Pts',(-21.0043775797276,-18.4828058803714,
22.));
#207060=CARTESIAN_POINT('Ctrl Pts',(-21.007836047032,-18.5172427598331,
22.));
#207061=CARTESIAN_POINT('Ctrl Pts',(-21.0104936869016,-18.5518107962264,
22.));
#207062=CARTESIAN_POINT('Ctrl Pts',(-21.012353412468,-18.5864814607357,
22.));
#207063=CARTESIAN_POINT('Ctrl Pts',(-21.0130853706128,-18.6001272780164,
22.));
#207064=CARTESIAN_POINT('Ctrl Pts',(-21.013693711025,-18.613790984168,22.));
#207065=CARTESIAN_POINT('Ctrl Pts',(-21.0141781405805,-18.6274531823049,
22.));
#207066=CARTESIAN_POINT('Ctrl Pts',(-21.0170629011428,-18.7088110803349,
22.));
#207067=CARTESIAN_POINT('Ctrl Pts',(-21.0155663446046,-18.7902456314198,
22.));
#207068=CARTESIAN_POINT('Ctrl Pts',(-21.0098210964673,-18.8713996487605,
22.));
#207069=CARTESIAN_POINT('Ctrl Pts',(-21.0040551877172,-18.9528455058409,
22.));
#207070=CARTESIAN_POINT('Ctrl Pts',(-20.9940096006406,-19.0340098256051,
22.));
#207071=CARTESIAN_POINT('Ctrl Pts',(-20.9797677148141,-19.1145199799703,
22.));
#207072=CARTESIAN_POINT('Ctrl Pts',(-20.9656475419077,-19.1943420845851,
22.));
#207073=CARTESIAN_POINT('Ctrl Pts',(-20.9474020500803,-19.2735220803298,
22.));
#207074=CARTESIAN_POINT('Ctrl Pts',(-20.9250689726277,-19.3516710302886,
22.));
#207075=CARTESIAN_POINT('Ctrl Pts',(-20.9157717541756,-19.3842042922679,
22.));
#207076=CARTESIAN_POINT('Ctrl Pts',(-20.9057656547729,-19.4165584812898,
22.));
#207077=CARTESIAN_POINT('Ctrl Pts',(-20.8950514146661,-19.4487036278629,
22.));
#207078=CARTESIAN_POINT('Ctrl Pts',(-20.8895107411906,-19.4653269029819,
22.));
#207079=CARTESIAN_POINT('Ctrl Pts',(-20.8837798105413,-19.4818963067406,
22.));
#207080=CARTESIAN_POINT('Ctrl Pts',(-20.8778666083137,-19.4983863278128,
22.));
#207081=CARTESIAN_POINT('Ctrl Pts',(-20.8511334402601,-19.5729365440179,
22.));
#207082=CARTESIAN_POINT('Ctrl Pts',(-20.8206473963515,-19.6459626051822,
22.));
#207083=CARTESIAN_POINT('Ctrl Pts',(-20.7864673296103,-19.7171052508947,
22.));
#207084=CARTESIAN_POINT('Ctrl Pts',(-20.7601551154116,-19.7718716896741,
22.));
#207085=CARTESIAN_POINT('Ctrl Pts',(-20.7316528766953,-19.8255216226873,
22.));
#207086=CARTESIAN_POINT('Ctrl Pts',(-20.7009722593753,-19.8778764706885,
22.));
#207087=CARTESIAN_POINT('Ctrl Pts',(-20.691737989898,-19.893634262321,22.));
#207088=CARTESIAN_POINT('Ctrl Pts',(-20.6823062983705,-19.9092746300216,
22.));
#207089=CARTESIAN_POINT('Ctrl Pts',(-20.6726772909679,-19.9247924234514,
22.));
#207090=CARTESIAN_POINT('Ctrl Pts',(-20.6644523795805,-19.9380474216617,
22.));
#207091=CARTESIAN_POINT('Ctrl Pts',(-20.6560857687532,-19.9512092205436,
22.));
#207092=CARTESIAN_POINT('Ctrl Pts',(-20.6475820686168,-19.9642683076145,
22.));
#207093=CARTESIAN_POINT('Ctrl Pts',(-20.6064305516755,-20.0274644733087,
22.));
#207094=CARTESIAN_POINT('Ctrl Pts',(-20.5620419166415,-20.0883056868183,
22.));
#207095=CARTESIAN_POINT('Ctrl Pts',(-20.5144495392311,-20.1464522171398,
22.));
#207096=CARTESIAN_POINT('Ctrl Pts',(-20.4703172870206,-20.2003713000043,
22.));
#207097=CARTESIAN_POINT('Ctrl Pts',(-20.4234296568856,-20.2519733998006,
22.));
#207098=CARTESIAN_POINT('Ctrl Pts',(-20.3737906915119,-20.3009544512441,
22.));
#207099=CARTESIAN_POINT('Ctrl Pts',(-20.368202130628,-20.3064689414452,
22.));
#207100=CARTESIAN_POINT('Ctrl Pts',(-20.3625786754248,-20.3119501712233,
22.));
#207101=CARTESIAN_POINT('Ctrl Pts',(-20.3569206944252,-20.3173979915434,
22.));
#207102=CARTESIAN_POINT('Ctrl Pts',(-23.5309290705171,12.9159954693336,
3.78082017782678));
#207103=CARTESIAN_POINT('Ctrl Pts',(-23.4921433079708,12.3929904264528,
3.32811049525756));
#207104=CARTESIAN_POINT('Ctrl Pts',(-23.4145756637886,11.1227341693237,
2.68282848235636));
#207105=CARTESIAN_POINT('Ctrl Pts',(-23.2982261379702,8.98514974237196,
2.72043101044529));
#207106=CARTESIAN_POINT('Ctrl Pts',(-23.181880493062,7.11443374085103,3.7545041503849));
#207107=CARTESIAN_POINT('Ctrl Pts',(-23.0655348481538,5.94558822129673,
5.54427718926393));
#207108=CARTESIAN_POINT('Ctrl Pts',(-22.9491892032456,5.75102063216925,
7.67300413669454));
#207109=CARTESIAN_POINT('Ctrl Pts',(-22.8328435583374,6.57591665960292,
9.64502733133667));
#207110=CARTESIAN_POINT('Ctrl Pts',(-22.7164979134292,8.2282608210192,11.0011717427377));
#207111=CARTESIAN_POINT('Ctrl Pts',(-22.600152268521,10.323288213565,11.4256682689063));
#207112=CARTESIAN_POINT('Ctrl Pts',(-22.4838066236128,12.3731970142136,
10.8196752010624));
#207113=CARTESIAN_POINT('Ctrl Pts',(-22.3674609787046,13.9006736370829,
9.32429434527451));
#207114=CARTESIAN_POINT('Ctrl Pts',(-22.2511153337964,14.5500550456883,
7.28771604356662));
#207115=CARTESIAN_POINT('Ctrl Pts',(-22.1347696888882,14.1701406045664,
5.18414452104409));
#207116=CARTESIAN_POINT('Ctrl Pts',(-22.01842404398,12.8493807879515,3.50338441272897));
#207117=CARTESIAN_POINT('Ctrl Pts',(-21.9020783990718,10.8953289008482,
2.63678819422404));
#207118=CARTESIAN_POINT('Ctrl Pts',(-21.7857327541637,8.76292617796746,
2.78614191158665));
#207119=CARTESIAN_POINT('Ctrl Pts',(-21.6693871092554,6.94878938547822,
3.9166601151248));
#207120=CARTESIAN_POINT('Ctrl Pts',(-21.5530414643472,5.87511984341867,
5.76512820704877));
#207121=CARTESIAN_POINT('Ctrl Pts',(-21.436695819439,5.79235256012249,7.90110085502655));
#207122=CARTESIAN_POINT('Ctrl Pts',(-21.3203501745309,6.71884383786294,
9.82731569971233));
#207123=CARTESIAN_POINT('Ctrl Pts',(-21.2040045296227,8.44078094673926,
11.0950863074763));
#207124=CARTESIAN_POINT('Ctrl Pts',(-21.0876588847145,10.5532155549212,
11.4095949826005));
#207125=CARTESIAN_POINT('Ctrl Pts',(-20.9713132398063,12.5726553215346,
10.6968254724326));
#207126=CARTESIAN_POINT('Ctrl Pts',(-20.8549675948981,14.0113681472882,
9.12439137309156));
#207127=CARTESIAN_POINT('Ctrl Pts',(-20.6998400683538,14.7564835991063,
6.36487657912614));
#207128=CARTESIAN_POINT('Ctrl Pts',(-20.5059306601735,12.9941084081549,
2.90529953905878));
#207129=CARTESIAN_POINT('Ctrl Pts',(-20.2732393703571,8.33351686037291,
2.33663235857614));
#207130=CARTESIAN_POINT('Ctrl Pts',(-20.0793299621768,5.79098465748635,
5.27094140963515));
#207131=CARTESIAN_POINT('Ctrl Pts',(-19.9242024356325,5.85070730033819,
8.1286594049214));
#207132=CARTESIAN_POINT('Ctrl Pts',(-19.8078567907243,6.8691141699218,10.0009016541358));
#207133=CARTESIAN_POINT('Ctrl Pts',(-19.6915111458161,8.65791837240851,
11.1783382217567));
#207134=CARTESIAN_POINT('Ctrl Pts',(-19.5751655009079,10.7840004919133,
11.3809968058206));
#207135=CARTESIAN_POINT('Ctrl Pts',(-19.4588198559997,12.7602560148627,
10.5644652210994));
#207136=CARTESIAN_POINT('Ctrl Pts',(-19.3424742110915,14.1227278031238,
8.91754071104751));
#207137=CARTESIAN_POINT('Ctrl Pts',(-19.2261285661833,14.5559884821405,
6.82433389849613));
#207138=CARTESIAN_POINT('Ctrl Pts',(-19.1097829212752,13.9582878934289,
4.77193175011942));
#207139=CARTESIAN_POINT('Ctrl Pts',(-18.993437276367,12.4692119255032,3.23836842500364));
#207140=CARTESIAN_POINT('Ctrl Pts',(-18.8770916314588,10.4352843405056,
2.58065535350108));
#207141=CARTESIAN_POINT('Ctrl Pts',(-18.7607459865506,8.3301873937482,2.95197008276899));
#207142=CARTESIAN_POINT('Ctrl Pts',(-18.6444003416424,6.64403470258783,
4.26583846924497));
#207143=CARTESIAN_POINT('Ctrl Pts',(-18.5280546967342,5.76945787151179,
6.21634186567518));
#207144=CARTESIAN_POINT('Ctrl Pts',(-18.411709051826,5.91008699804141,8.34931416779286));
#207145=CARTESIAN_POINT('Ctrl Pts',(-18.2953634069178,7.03318105231844,
10.1681073068047));
#207146=CARTESIAN_POINT('Ctrl Pts',(-18.1790177620096,8.87723500286934,
11.2492265031511));
#207147=CARTESIAN_POINT('Ctrl Pts',(-18.0626721171014,11.0128674555704,
11.3409385700576));
#207148=CARTESIAN_POINT('Ctrl Pts',(-17.9463264721932,12.9428215115083,
10.4218921978272));
#207149=CARTESIAN_POINT('Ctrl Pts',(-17.829980827285,14.2176934838242,8.70607449466463));
#207150=CARTESIAN_POINT('Ctrl Pts',(-17.7136351823768,14.5406917268196,
6.59301815408165));
#207151=CARTESIAN_POINT('Ctrl Pts',(-17.5972895374686,13.8364941704587,
4.57470371354082));
#207152=CARTESIAN_POINT('Ctrl Pts',(-17.4809438925604,12.2693085317063,
3.12115124087976));
#207153=CARTESIAN_POINT('Ctrl Pts',(-17.3645982476522,10.2035493395539,
2.57068309301411));
#207154=CARTESIAN_POINT('Ctrl Pts',(-17.2870344843801,8.81547162341348,
2.89154656229486));
#207155=CARTESIAN_POINT('Ctrl Pts',(-17.248252602744,8.19900211022411,3.20515433429992));
#207156=CARTESIAN_POINT('Ctrl Pts',(-23.6935174548172,13.1003005986416,
3.5678963242189));
#207157=CARTESIAN_POINT('Ctrl Pts',(-23.654731692271,12.5427028162004,3.08524339662984));
#207158=CARTESIAN_POINT('Ctrl Pts',(-23.5771640480887,11.1884289296508,
2.39728096808227));
#207159=CARTESIAN_POINT('Ctrl Pts',(-23.4608145222703,8.90945982127682,
2.43737061265066));
#207160=CARTESIAN_POINT('Ctrl Pts',(-23.3444688773622,6.91501042117213,
3.53983969504486));
#207161=CARTESIAN_POINT('Ctrl Pts',(-23.2281232324539,5.66885480835072,
5.44799238140327));
#207162=CARTESIAN_POINT('Ctrl Pts',(-23.1117775875458,5.46141807765529,
7.71751815647438));
#207163=CARTESIAN_POINT('Ctrl Pts',(-22.9954319426376,6.34087459896918,
9.81997543718874));
#207164=CARTESIAN_POINT('Ctrl Pts',(-22.8790862977294,8.10250855026048,
11.2658183153034));
#207165=CARTESIAN_POINT('Ctrl Pts',(-22.7627406528212,10.3361058054659,
11.7183920043482));
#207166=CARTESIAN_POINT('Ctrl Pts',(-22.646395007913,12.5216002227899,11.0723171807799));
#207167=CARTESIAN_POINT('Ctrl Pts',(-22.5300493630048,14.1501076133713,
9.47802844409872));
#207168=CARTESIAN_POINT('Ctrl Pts',(-22.4137037180966,14.8424405809512,
7.30674623514494));
#207169=CARTESIAN_POINT('Ctrl Pts',(-22.2973580731884,14.4373977371574,
5.06403972183058));
#207170=CARTESIAN_POINT('Ctrl Pts',(-22.1810124282802,13.02927987117,3.27211032847339));
#207171=CARTESIAN_POINT('Ctrl Pts',(-22.064666783372,10.9459825610289,2.34819547088681));
#207172=CARTESIAN_POINT('Ctrl Pts',(-21.9483211384638,8.67253788638379,
2.50742778180684));
#207173=CARTESIAN_POINT('Ctrl Pts',(-21.8319754935556,6.73840997250145,
3.71272102301552));
#207174=CARTESIAN_POINT('Ctrl Pts',(-21.7156298486474,5.59372549215789,
5.68345098633069));
#207175=CARTESIAN_POINT('Ctrl Pts',(-21.5992842037392,5.50548379305222,
7.96070170901428));
#207176=CARTESIAN_POINT('Ctrl Pts',(-21.482938558831,6.49325530491686,10.0143207716261));
#207177=CARTESIAN_POINT('Ctrl Pts',(-21.3665929139228,8.3290852390299,11.3659446023248));
#207178=CARTESIAN_POINT('Ctrl Pts',(-21.2502472690146,10.581241062588,11.7012555944365));
#207179=CARTESIAN_POINT('Ctrl Pts',(-21.1339016241064,12.734251154871,10.9413418925109));
#207180=CARTESIAN_POINT('Ctrl Pts',(-21.0175559791982,14.2681237095048,
9.26490343601343));
#207181=CARTESIAN_POINT('Ctrl Pts',(-20.862428452654,15.0625227870125,6.32286807579321));
#207182=CARTESIAN_POINT('Ctrl Pts',(-20.6685190444737,13.1835801043741,
2.63446676497503));
#207183=CARTESIAN_POINT('Ctrl Pts',(-20.4358277546573,8.21472646274736,
2.02818664760248));
#207184=CARTESIAN_POINT('Ctrl Pts',(-20.2419183464769,5.50402541423371,
5.15657755346331));
#207185=CARTESIAN_POINT('Ctrl Pts',(-20.0867908199327,5.56769824811748,
8.2033114974362));
#207186=CARTESIAN_POINT('Ctrl Pts',(-19.9704451750245,6.65346485750777,
10.1993880947178));
#207187=CARTESIAN_POINT('Ctrl Pts',(-19.8540995301163,8.56058462643782,
11.454702987007));
#207188=CARTESIAN_POINT('Ctrl Pts',(-19.7377538852081,10.8272906386664,
11.6707658693921));
#207189=CARTESIAN_POINT('Ctrl Pts',(-19.6214082402999,12.9342601834799,
10.8002270339997));
#207190=CARTESIAN_POINT('Ctrl Pts',(-19.5050625953917,14.3868489455089,
9.04437120210426));
#207191=CARTESIAN_POINT('Ctrl Pts',(-19.3887169504835,14.8487664683456,
6.81271494418272));
#207192=CARTESIAN_POINT('Ctrl Pts',(-19.2723713055753,14.2115326072846,
4.62456226345754));
#207193=CARTESIAN_POINT('Ctrl Pts',(-19.1560256606671,12.6239657780463,
2.98956558234025));
#207194=CARTESIAN_POINT('Ctrl Pts',(-19.0396800157589,10.4555096102171,
2.28834987678537));
#207195=CARTESIAN_POINT('Ctrl Pts',(-18.9233343708507,8.2111767776498,2.68422420428154));
#207196=CARTESIAN_POINT('Ctrl Pts',(-18.8069887259426,6.41349812378914,
4.08499482531277));
#207197=CARTESIAN_POINT('Ctrl Pts',(-18.6906430810343,5.48107479781828,
6.1645089395608));
#207198=CARTESIAN_POINT('Ctrl Pts',(-18.5742974361261,5.63100545368278,
8.43856086670521));
#207199=CARTESIAN_POINT('Ctrl Pts',(-18.457951791218,6.82838349556238,10.3776531084284));
#207200=CARTESIAN_POINT('Ctrl Pts',(-18.3416061463098,8.79440735618407,
11.530279980087));
#207201=CARTESIAN_POINT('Ctrl Pts',(-18.2252605014016,11.071295382304,11.6280580910751));
#207202=CARTESIAN_POINT('Ctrl Pts',(-18.1089148564934,13.1289009760795,
10.6482239076538));
#207203=CARTESIAN_POINT('Ctrl Pts',(-17.9925692115852,14.4880958716855,
8.81891813062558));
#207204=CARTESIAN_POINT('Ctrl Pts',(-17.876223566677,14.8324579509393,6.56609945187542));
#207205=CARTESIAN_POINT('Ctrl Pts',(-17.7598779217688,14.0816831712841,
4.41428911728345));
#207206=CARTESIAN_POINT('Ctrl Pts',(-17.6435322768606,12.4108403204606,
2.86459538784371));
#207207=CARTESIAN_POINT('Ctrl Pts',(-17.5271866319524,10.2084471307945,
2.27771802837559));
#207208=CARTESIAN_POINT('Ctrl Pts',(-17.4496228686803,8.7285588067495,2.61980413514017));
#207209=CARTESIAN_POINT('Ctrl Pts',(-17.4108409870442,8.07131460198311,
2.95415463635743));
#207210=CARTESIAN_POINT('Ctrl Pts',(-23.8561058391174,13.2846057279496,
3.35497247061101));
#207211=CARTESIAN_POINT('Ctrl Pts',(-23.8173200765711,12.692415205948,2.84237629800212));
#207212=CARTESIAN_POINT('Ctrl Pts',(-23.7397524323889,11.2541236899778,
2.11173345380816));
#207213=CARTESIAN_POINT('Ctrl Pts',(-23.6234029065705,8.83376990018168,
2.15431021485603));
#207214=CARTESIAN_POINT('Ctrl Pts',(-23.5070572616623,6.71558710149322,
3.32517523970482));
#207215=CARTESIAN_POINT('Ctrl Pts',(-23.3907116167541,5.39212139540471,
5.35170757354262));
#207216=CARTESIAN_POINT('Ctrl Pts',(-23.2743659718459,5.17181552314134,
7.76203217625421));
#207217=CARTESIAN_POINT('Ctrl Pts',(-23.1580203269378,6.10583253833545,
9.99492354304081));
#207218=CARTESIAN_POINT('Ctrl Pts',(-23.0416746820295,7.97675627950178,
11.5304648878691));
#207219=CARTESIAN_POINT('Ctrl Pts',(-22.9253290371214,10.3489233973667,
12.0111157397901));
#207220=CARTESIAN_POINT('Ctrl Pts',(-22.8089833922131,12.6700034313663,
11.3249591604974));
#207221=CARTESIAN_POINT('Ctrl Pts',(-22.692637747305,14.3995415896597,9.63176254292293));
#207222=CARTESIAN_POINT('Ctrl Pts',(-22.5762921023967,15.1348261162141,
7.32577642672326));
#207223=CARTESIAN_POINT('Ctrl Pts',(-22.4599464574886,14.7046548697485,
4.94393492261707));
#207224=CARTESIAN_POINT('Ctrl Pts',(-22.3436008125804,13.2091789543886,
3.04083624421781));
#207225=CARTESIAN_POINT('Ctrl Pts',(-22.2272551676722,10.9966362212096,
2.05960274754957));
#207226=CARTESIAN_POINT('Ctrl Pts',(-22.110909522764,8.58214959480014,2.22871365202703));
#207227=CARTESIAN_POINT('Ctrl Pts',(-21.9945638778558,6.52803055952468,
3.50878193090623));
#207228=CARTESIAN_POINT('Ctrl Pts',(-21.8782182329476,5.31233114089711,
5.60177376561261));
#207229=CARTESIAN_POINT('Ctrl Pts',(-21.7618725880394,5.21861502598196,
8.02030256300201));
#207230=CARTESIAN_POINT('Ctrl Pts',(-21.6455269431312,6.26766677197077,
10.2013258435399));
#207231=CARTESIAN_POINT('Ctrl Pts',(-21.529181298223,8.21738953132054,11.6368028971734));
#207232=CARTESIAN_POINT('Ctrl Pts',(-21.4128356533148,10.6092665702549,
11.9929162062726));
#207233=CARTESIAN_POINT('Ctrl Pts',(-21.2964900084066,12.8958469882074,
11.1858583125893));
#207234=CARTESIAN_POINT('Ctrl Pts',(-21.1801443634984,14.5248792717214,
9.4054154989353));
#207235=CARTESIAN_POINT('Ctrl Pts',(-21.0250168369542,15.3685619749188,
6.28085957246028));
#207236=CARTESIAN_POINT('Ctrl Pts',(-20.8311074287738,13.3730518005934,
2.36363399089129));
#207237=CARTESIAN_POINT('Ctrl Pts',(-20.5984161389574,8.09593606512178,
1.71974093662882));
#207238=CARTESIAN_POINT('Ctrl Pts',(-20.4045067307771,5.21706617098109,
5.04221369729146));
#207239=CARTESIAN_POINT('Ctrl Pts',(-20.2493792042329,5.28468919589676,
8.277963589951));
#207240=CARTESIAN_POINT('Ctrl Pts',(-20.1330335593247,6.43781554509373,
10.3978745352999));
#207241=CARTESIAN_POINT('Ctrl Pts',(-20.0166879144165,8.46325088046714,
11.7310677522574));
#207242=CARTESIAN_POINT('Ctrl Pts',(-19.9003422695083,10.8705807854194,
11.9605349329635));
#207243=CARTESIAN_POINT('Ctrl Pts',(-19.7839966246001,13.1082643520972,
11.0359888469001));
#207244=CARTESIAN_POINT('Ctrl Pts',(-19.6676509796919,14.6509700878939,
9.17120169316103));
#207245=CARTESIAN_POINT('Ctrl Pts',(-19.5513053347837,15.1415444545508,
6.80109598986931));
#207246=CARTESIAN_POINT('Ctrl Pts',(-19.4349596898755,14.4647773211402,
4.47719277679566));
#207247=CARTESIAN_POINT('Ctrl Pts',(-19.3186140449673,12.7787196305894,
2.74076273967685));
#207248=CARTESIAN_POINT('Ctrl Pts',(-19.2022684000591,10.4757348799287,
1.99604440006967));
#207249=CARTESIAN_POINT('Ctrl Pts',(-19.0859227551509,8.09216616155139,
2.41647832579409));
#207250=CARTESIAN_POINT('Ctrl Pts',(-18.9695771102427,6.18296154499045,
3.90415118138058));
#207251=CARTESIAN_POINT('Ctrl Pts',(-18.8532314653345,5.19269172412475,
6.11267601344642));
#207252=CARTESIAN_POINT('Ctrl Pts',(-18.7368858204263,5.35192390932415,
8.52780756561754));
#207253=CARTESIAN_POINT('Ctrl Pts',(-18.6205401755181,6.62358593880632,
10.5871989100521));
#207254=CARTESIAN_POINT('Ctrl Pts',(-18.5041945306099,8.7115797094988,11.811333457023));
#207255=CARTESIAN_POINT('Ctrl Pts',(-18.3878488857017,11.1297233090374,
11.9151776120927));
#207256=CARTESIAN_POINT('Ctrl Pts',(-18.2715032407935,13.3149804406506,
10.8745556174806));
#207257=CARTESIAN_POINT('Ctrl Pts',(-18.1551575958854,14.7584982595467,
8.93176176658652));
#207258=CARTESIAN_POINT('Ctrl Pts',(-18.0388119509771,15.124224175059,6.53918074966919));
#207259=CARTESIAN_POINT('Ctrl Pts',(-17.922466306069,14.3268721721096,4.25387452102607));
#207260=CARTESIAN_POINT('Ctrl Pts',(-17.8061206611608,12.5523721092149,
2.60803953480767));
#207261=CARTESIAN_POINT('Ctrl Pts',(-17.6897750162526,10.2133449220351,
1.98475296373708));
#207262=CARTESIAN_POINT('Ctrl Pts',(-17.6122112529804,8.64164599008553,
2.34806170798548));
#207263=CARTESIAN_POINT('Ctrl Pts',(-17.5734293713444,7.94362709374212,
2.70315493841493));
#207264=CARTESIAN_POINT('Ctrl Pts',(-24.0186942234176,13.4689108572577,
3.14204861700312));
#207265=CARTESIAN_POINT('Ctrl Pts',(-23.9799084608713,12.8421275956956,
2.59950919937439));
#207266=CARTESIAN_POINT('Ctrl Pts',(-23.9023408166891,11.3198184503049,
1.82618593953407));
#207267=CARTESIAN_POINT('Ctrl Pts',(-23.7859912908707,8.75807997908655,
1.8712498170614));
#207268=CARTESIAN_POINT('Ctrl Pts',(-23.6696456459625,6.51616378181432,
3.11051078436478));
#207269=CARTESIAN_POINT('Ctrl Pts',(-23.5533000010543,5.1153879824587,5.25542276568198));
#207270=CARTESIAN_POINT('Ctrl Pts',(-23.4369543561461,4.88221296862737,
7.80654619603404));
#207271=CARTESIAN_POINT('Ctrl Pts',(-23.3206087112379,5.87079047770171,
10.1698716488929));
#207272=CARTESIAN_POINT('Ctrl Pts',(-23.2042630663297,7.85100400874307,
11.7951114604348));
#207273=CARTESIAN_POINT('Ctrl Pts',(-23.0879174214215,10.3617409892675,
12.3038394752319));
#207274=CARTESIAN_POINT('Ctrl Pts',(-22.9715717765133,12.8184066399426,
11.5776011402149));
#207275=CARTESIAN_POINT('Ctrl Pts',(-22.8552261316051,14.6489755659482,
9.78549664174713));
#207276=CARTESIAN_POINT('Ctrl Pts',(-22.7388804866969,15.427211651477,7.34480661830159));
#207277=CARTESIAN_POINT('Ctrl Pts',(-22.6225348417888,14.9719120023394,
4.82383012340355));
#207278=CARTESIAN_POINT('Ctrl Pts',(-22.5061891968806,13.3890780376071,
2.80956215996224));
#207279=CARTESIAN_POINT('Ctrl Pts',(-22.3898435519723,11.0472898813903,
1.77101002421233));
#207280=CARTESIAN_POINT('Ctrl Pts',(-22.2734979070642,8.49176130321648,
1.94999952224723));
#207281=CARTESIAN_POINT('Ctrl Pts',(-22.157152262156,6.3176511465479,3.30484283879696));
#207282=CARTESIAN_POINT('Ctrl Pts',(-22.0408066172478,5.03093678963633,
5.52009654489452));
#207283=CARTESIAN_POINT('Ctrl Pts',(-21.9244609723396,4.93174625891169,
8.07990341698975));
#207284=CARTESIAN_POINT('Ctrl Pts',(-21.8081153274314,6.04207823902469,
10.3883309154536));
#207285=CARTESIAN_POINT('Ctrl Pts',(-21.6917696825232,8.10569382361118,
11.9076611920219));
#207286=CARTESIAN_POINT('Ctrl Pts',(-21.575424037615,10.6372920779218,12.2845768181086));
#207287=CARTESIAN_POINT('Ctrl Pts',(-21.4590783927068,13.0574428215438,
11.4303747326676));
#207288=CARTESIAN_POINT('Ctrl Pts',(-21.3427327477986,14.7816348339379,
9.54592756185717));
#207289=CARTESIAN_POINT('Ctrl Pts',(-21.1876052212543,15.6746011628252,
6.23885106912733));
#207290=CARTESIAN_POINT('Ctrl Pts',(-20.993695813074,13.5625234968125,2.09280121680755));
#207291=CARTESIAN_POINT('Ctrl Pts',(-20.7610045232576,7.9771456674962,1.41129522565514));
#207292=CARTESIAN_POINT('Ctrl Pts',(-20.5670951150773,4.93010692772846,
4.92784984111965));
#207293=CARTESIAN_POINT('Ctrl Pts',(-20.411967588533,5.00168014367605,8.35261568246579));
#207294=CARTESIAN_POINT('Ctrl Pts',(-20.2956219436248,6.22216623267968,
10.5963609758821));
#207295=CARTESIAN_POINT('Ctrl Pts',(-20.1792762987167,8.36591713449647,
12.0074325175077));
#207296=CARTESIAN_POINT('Ctrl Pts',(-20.0629306538084,10.9138709321725,
12.250303996535));
#207297=CARTESIAN_POINT('Ctrl Pts',(-19.9465850089003,13.2822685207144,
11.2717506598004));
#207298=CARTESIAN_POINT('Ctrl Pts',(-19.8302393639921,14.915091230279,9.29803218421779));
#207299=CARTESIAN_POINT('Ctrl Pts',(-19.7138937190839,15.4343224407561,
6.7894770355559));
#207300=CARTESIAN_POINT('Ctrl Pts',(-19.5975480741757,14.7180220349959,
4.32982329013379));
#207301=CARTESIAN_POINT('Ctrl Pts',(-19.4812024292675,12.9334734831326,
2.49195989701346));
#207302=CARTESIAN_POINT('Ctrl Pts',(-19.3648567843593,10.4959601496402,
1.70373892335395));
#207303=CARTESIAN_POINT('Ctrl Pts',(-19.2485111394511,7.97315554545298,
2.14873244730664));
#207304=CARTESIAN_POINT('Ctrl Pts',(-19.1321654945429,5.95242496619178,
3.72330753744839));
#207305=CARTESIAN_POINT('Ctrl Pts',(-19.0158198496347,4.90430865043124,
6.06084308733203));
#207306=CARTESIAN_POINT('Ctrl Pts',(-18.8994742047265,5.07284236496551,
8.61705426452988));
#207307=CARTESIAN_POINT('Ctrl Pts',(-18.7831285598183,6.41878838205027,
10.7967447116758));
#207308=CARTESIAN_POINT('Ctrl Pts',(-18.6667829149101,8.62875206281352,
12.0923869339589));
#207309=CARTESIAN_POINT('Ctrl Pts',(-18.5504372700019,11.1881512357709,
12.2022971331103));
#207310=CARTESIAN_POINT('Ctrl Pts',(-18.4340916250937,13.5010599052218,
11.1008873273073));
#207311=CARTESIAN_POINT('Ctrl Pts',(-18.3177459801855,15.0289006474081,
9.04460540254747));
#207312=CARTESIAN_POINT('Ctrl Pts',(-18.2014003352773,15.4159903991786,
6.51226204746295));
#207313=CARTESIAN_POINT('Ctrl Pts',(-18.0850546903691,14.572061172935,4.09345992476871));
#207314=CARTESIAN_POINT('Ctrl Pts',(-17.968709045461,12.6939038979692,2.35148368177163));
#207315=CARTESIAN_POINT('Ctrl Pts',(-17.8523634005528,10.2182427132757,
1.69178789909856));
#207316=CARTESIAN_POINT('Ctrl Pts',(-17.7747996372806,8.55473317342155,
2.07631928083078));
#207317=CARTESIAN_POINT('Ctrl Pts',(-17.7360177556446,7.81593958550113,
2.45215524047243));
#207318=CARTESIAN_POINT('Ctrl Pts',(-17.734,7.81752421401937,2.45527019889639));
#207319=CARTESIAN_POINT('Ctrl Pts',(-17.734,7.95501332932839,2.39880616079669));
#207320=CARTESIAN_POINT('Ctrl Pts',(-17.734,8.09483307093976,2.34855996252215));
#207321=CARTESIAN_POINT('Ctrl Pts',(-17.734,8.23654961332729,2.30458248664204));
#207322=CARTESIAN_POINT('Ctrl Pts',(-17.734,8.37832975980054,2.26058527314275));
#207323=CARTESIAN_POINT('Ctrl Pts',(-17.734,8.5220092129709,2.22286236358206));
#207324=CARTESIAN_POINT('Ctrl Pts',(-17.734,8.66715872383441,2.19151622076045));
#207325=CARTESIAN_POINT('Ctrl Pts',(-17.734,8.73062405339664,2.17781039927443));
#207326=CARTESIAN_POINT('Ctrl Pts',(-17.734,8.79437042278305,2.16532435435612));
#207327=CARTESIAN_POINT('Ctrl Pts',(-17.734,8.85836166295589,2.15406978045215));
#207328=CARTESIAN_POINT('Ctrl Pts',(-17.734,8.89040869116538,2.1484334520045));
#207329=CARTESIAN_POINT('Ctrl Pts',(-17.734,8.92251712887927,2.14310601138362));
#207330=CARTESIAN_POINT('Ctrl Pts',(-17.734,8.95468239459414,2.13808910834503));
#207331=CARTESIAN_POINT('Ctrl Pts',(-17.734,8.98448154611367,2.13344125450384));
#207332=CARTESIAN_POINT('Ctrl Pts',(-17.734,9.01432763207528,2.12906034005483));
#207333=CARTESIAN_POINT('Ctrl Pts',(-17.734,9.04419731217815,2.12495001471572));
#207334=CARTESIAN_POINT('Ctrl Pts',(-17.734,9.18914015359341,2.10500463091048));
#207335=CARTESIAN_POINT('Ctrl Pts',(-17.734,9.33476319047707,2.09140666582529));
#207336=CARTESIAN_POINT('Ctrl Pts',(-17.734,9.48065042400814,2.08424512748072));
#207337=CARTESIAN_POINT('Ctrl Pts',(-17.734,9.62430709149771,2.07719308661478));
#207338=CARTESIAN_POINT('Ctrl Pts',(-17.734,9.76822064463766,2.07638225413551));
#207339=CARTESIAN_POINT('Ctrl Pts',(-17.734,9.91198516113969,2.08194693816168));
#207340=CARTESIAN_POINT('Ctrl Pts',(-17.734,9.99104601856735,2.085007141758));
#207341=CARTESIAN_POINT('Ctrl Pts',(-17.734,10.0700615881095,2.08999633226591));
#207342=CARTESIAN_POINT('Ctrl Pts',(-17.734,10.1489620547016,2.09694320736949));
#207343=CARTESIAN_POINT('Ctrl Pts',(-17.734,10.1675473093435,2.09857956578842));
#207344=CARTESIAN_POINT('Ctrl Pts',(-17.734,10.1861239058425,2.10032440268515));
#207345=CARTESIAN_POINT('Ctrl Pts',(-17.734,10.204682003642,2.10217705470482));
#207346=CARTESIAN_POINT('Ctrl Pts',(-17.734,10.2069686559161,2.10240533084603));
#207347=CARTESIAN_POINT('Ctrl Pts',(-17.734,10.2092550663573,2.10263524723068));
#207348=CARTESIAN_POINT('Ctrl Pts',(-17.734,10.2115412333789,2.10286680408659));
#207349=CARTESIAN_POINT('Ctrl Pts',(-17.734,10.3540154766321,2.11729745919824));
#207350=CARTESIAN_POINT('Ctrl Pts',(-17.734,10.4955450211138,2.13809494422707));
#207351=CARTESIAN_POINT('Ctrl Pts',(-17.734,10.6357416460623,2.16507440736953));
#207352=CARTESIAN_POINT('Ctrl Pts',(-17.734,10.7763962044029,2.19214199529445));
#207353=CARTESIAN_POINT('Ctrl Pts',(-17.734,10.9157098757399,2.22543235083154));
#207354=CARTESIAN_POINT('Ctrl Pts',(-17.734,11.0532754222464,2.26480926967513));
#207355=CARTESIAN_POINT('Ctrl Pts',(-17.734,11.1892331875549,2.30372597539589));
#207356=CARTESIAN_POINT('Ctrl Pts',(-17.734,11.3234841067246,2.34858822550377));
#207357=CARTESIAN_POINT('Ctrl Pts',(-17.734,11.4556098131053,2.39930790766024));
#207358=CARTESIAN_POINT('Ctrl Pts',(-17.734,11.585893305135,2.44932041080583));
#207359=CARTESIAN_POINT('Ctrl Pts',(-17.734,11.7141110086898,2.50502853560071));
#207360=CARTESIAN_POINT('Ctrl Pts',(-17.734,11.8398280865206,2.56638422249516));
#207361=CARTESIAN_POINT('Ctrl Pts',(-17.734,11.8635810775125,2.57797676905487));
#207362=CARTESIAN_POINT('Ctrl Pts',(-17.734,11.8872446880899,2.58977102047971));
#207363=CARTESIAN_POINT('Ctrl Pts',(-17.734,11.9108158217838,2.60176678408464));
#207364=CARTESIAN_POINT('Ctrl Pts',(-17.734,11.9371259496047,2.61515646986953));
#207365=CARTESIAN_POINT('Ctrl Pts',(-17.734,11.9633250773611,2.62879964621102));
#207366=CARTESIAN_POINT('Ctrl Pts',(-17.734,11.989373711485,2.64267686049565));
#207367=CARTESIAN_POINT('Ctrl Pts',(-17.734,12.1092335086399,2.7065312676527));
#207368=CARTESIAN_POINT('Ctrl Pts',(-17.734,12.2260636232258,2.77541414480518));
#207369=CARTESIAN_POINT('Ctrl Pts',(-17.734,12.3395155043836,2.84921040440292));
#207370=CARTESIAN_POINT('Ctrl Pts',(-17.734,12.3590922141296,2.86194433124259));
#207371=CARTESIAN_POINT('Ctrl Pts',(-17.734,12.3785682723977,2.87482464861868));
#207372=CARTESIAN_POINT('Ctrl Pts',(-17.734,12.397941804336,2.88785087941439));
#207373=CARTESIAN_POINT('Ctrl Pts',(-17.734,12.5137183308796,2.96569583614642));
#207374=CARTESIAN_POINT('Ctrl Pts',(-17.734,12.6258364718941,3.04874887784061));
#207375=CARTESIAN_POINT('Ctrl Pts',(-17.734,12.7340053685887,3.13669684221419));
#207376=CARTESIAN_POINT('Ctrl Pts',(-17.734,12.8413651891311,3.22398697792551));
#207377=CARTESIAN_POINT('Ctrl Pts',(-17.734,12.9448350524763,3.31609977176641));
#207378=CARTESIAN_POINT('Ctrl Pts',(-17.734,13.0440889096738,3.41275801814899));
#207379=CARTESIAN_POINT('Ctrl Pts',(-17.734,13.1288759098258,3.49532773364548));
#207380=CARTESIAN_POINT('Ctrl Pts',(-17.734,13.2105858345473,3.58121510520998));
#207381=CARTESIAN_POINT('Ctrl Pts',(-17.734,13.2889874920904,3.67025872512399));
#207382=CARTESIAN_POINT('Ctrl Pts',(-17.734,13.3046808407887,3.68808223320354));
#207383=CARTESIAN_POINT('Ctrl Pts',(-17.734,13.3202415499158,3.70603222587404));
#207384=CARTESIAN_POINT('Ctrl Pts',(-17.734,13.3356676287495,3.72410744241816));
#207385=CARTESIAN_POINT('Ctrl Pts',(-17.734,13.3480960124007,3.73867016624531));
#207386=CARTESIAN_POINT('Ctrl Pts',(-17.734,13.3604375218648,3.75331488553882));
#207387=CARTESIAN_POINT('Ctrl Pts',(-17.734,13.3726806466598,3.76802811897179));
#207388=CARTESIAN_POINT('Ctrl Pts',(-17.734,13.4596595863362,3.87255547327408));
#207389=CARTESIAN_POINT('Ctrl Pts',(-17.734,13.5418047089289,3.98068713564632));
#207390=CARTESIAN_POINT('Ctrl Pts',(-17.734,13.6188521515589,4.09212747512559));
#207391=CARTESIAN_POINT('Ctrl Pts',(-17.734,13.6955050681823,4.20299717772703));
#207392=CARTESIAN_POINT('Ctrl Pts',(-17.734,13.7671127723517,4.31714241929128));
#207393=CARTESIAN_POINT('Ctrl Pts',(-17.734,13.8333700251483,4.43429573902715));
#207394=CARTESIAN_POINT('Ctrl Pts',(-17.734,13.8529952952312,4.46899632566313));
#207395=CARTESIAN_POINT('Ctrl Pts',(-17.734,13.8721508267902,4.50396094344829));
#207396=CARTESIAN_POINT('Ctrl Pts',(-17.734,13.89082783933,4.53918291414616));
#207397=CARTESIAN_POINT('Ctrl Pts',(-17.734,13.9541037547201,4.65851155051141));
#207398=CARTESIAN_POINT('Ctrl Pts',(-17.734,14.0118911506689,4.78079380916991));
#207399=CARTESIAN_POINT('Ctrl Pts',(-17.734,14.0640355569298,4.90562952893941));
#207400=CARTESIAN_POINT('Ctrl Pts',(-17.734,14.1069769502113,5.00843288068092));
#207401=CARTESIAN_POINT('Ctrl Pts',(-17.734,14.1460905703569,5.11296827640031));
#207402=CARTESIAN_POINT('Ctrl Pts',(-17.734,14.181263595494,5.21901089821796));
#207403=CARTESIAN_POINT('Ctrl Pts',(-17.734,14.189228939926,5.24302549474362));
#207404=CARTESIAN_POINT('Ctrl Pts',(-17.734,14.1969936498824,5.26712264831227));
#207405=CARTESIAN_POINT('Ctrl Pts',(-17.734,14.2045469401604,5.29126909440454));
#207406=CARTESIAN_POINT('Ctrl Pts',(-17.734,14.2441345445802,5.41782320802469));
#207407=CARTESIAN_POINT('Ctrl Pts',(-17.734,14.2779661336648,5.54586509835337));
#207408=CARTESIAN_POINT('Ctrl Pts',(-17.734,14.3059575691914,5.67500275481732));
#207409=CARTESIAN_POINT('Ctrl Pts',(-17.734,14.3337111014901,5.80304285180508));
#207410=CARTESIAN_POINT('Ctrl Pts',(-17.734,14.3557233452508,5.93216096675456));
#207411=CARTESIAN_POINT('Ctrl Pts',(-17.734,14.3718618342412,6.06197882819122));
#207412=CARTESIAN_POINT('Ctrl Pts',(-17.734,14.3878809810452,6.19083670214492));
#207413=CARTESIAN_POINT('Ctrl Pts',(-17.734,14.3981129478512,6.32038474523077));
#207414=CARTESIAN_POINT('Ctrl Pts',(-17.734,14.4023779577645,6.45024544035567));
#207415=CARTESIAN_POINT('Ctrl Pts',(-17.734,14.404077015673,6.50197822540308));
#207416=CARTESIAN_POINT('Ctrl Pts',(-17.734,14.4048285550272,6.55376048351597));
#207417=CARTESIAN_POINT('Ctrl Pts',(-17.734,14.4046189505891,6.60556761626202));
#207418=CARTESIAN_POINT('Ctrl Pts',(-17.734,14.4041999753073,6.7091241450779));
#207419=CARTESIAN_POINT('Ctrl Pts',(-17.734,14.3999416905426,6.8127807955209));
#207420=CARTESIAN_POINT('Ctrl Pts',(-17.734,14.3918515993157,6.91632173312881));
#207421=CARTESIAN_POINT('Ctrl Pts',(-23.534,12.9193325810254,3.77664721604209));
#207422=CARTESIAN_POINT('Ctrl Pts',(-23.534,12.8290342749467,3.68176973928167));
#207423=CARTESIAN_POINT('Ctrl Pts',(-23.534,12.7344699653718,3.59136003915295));
#207424=CARTESIAN_POINT('Ctrl Pts',(-23.534,12.6360835972834,3.50554511160901));
#207425=CARTESIAN_POINT('Ctrl Pts',(-23.534,12.5375436323605,3.41959621325707));
#207426=CARTESIAN_POINT('Ctrl Pts',(-23.534,12.4351690929809,3.33825596343349));
#207427=CARTESIAN_POINT('Ctrl Pts',(-23.534,12.3293560803945,3.26167549385161));
#207428=CARTESIAN_POINT('Ctrl Pts',(-23.534,12.2223961810542,3.18426498338892));
#207429=CARTESIAN_POINT('Ctrl Pts',(-23.534,12.111922327755,3.11171743092897));
#207430=CARTESIAN_POINT('Ctrl Pts',(-23.534,11.9983009629277,3.04422091350619));
#207431=CARTESIAN_POINT('Ctrl Pts',(-23.534,11.8876418446549,2.97848411201776));
#207432=CARTESIAN_POINT('Ctrl Pts',(-23.534,11.7739964774377,2.91753808376478));
#207433=CARTESIAN_POINT('Ctrl Pts',(-23.534,11.6576727871419,2.86159294221042));
#207434=CARTESIAN_POINT('Ctrl Pts',(-23.534,11.6332495630019,2.84984674736182));
#207435=CARTESIAN_POINT('Ctrl Pts',(-23.534,11.6087081820176,2.83832114633447));
#207436=CARTESIAN_POINT('Ctrl Pts',(-23.534,11.5840513615887,2.82701831535873));
#207437=CARTESIAN_POINT('Ctrl Pts',(-23.534,11.5622209636691,2.81701113302431));
#207438=CARTESIAN_POINT('Ctrl Pts',(-23.534,11.5402959333441,2.80717685242453));
#207439=CARTESIAN_POINT('Ctrl Pts',(-23.534,11.5183047885456,2.79752845804063));
#207440=CARTESIAN_POINT('Ctrl Pts',(-23.534,11.3911942477278,2.74175998216545));
#207441=CARTESIAN_POINT('Ctrl Pts',(-23.534,11.2617238431345,2.69212530511711));
#207442=CARTESIAN_POINT('Ctrl Pts',(-23.534,11.1303326631264,2.64879502193041));
#207443=CARTESIAN_POINT('Ctrl Pts',(-23.534,11.0033822809627,2.60692922843141));
#207444=CARTESIAN_POINT('Ctrl Pts',(-23.534,10.8746380135545,2.57094816886311));
#207445=CARTESIAN_POINT('Ctrl Pts',(-23.534,10.744524252389,2.54079174717232));
#207446=CARTESIAN_POINT('Ctrl Pts',(-23.534,10.6129949118458,2.51030723713584));
#207447=CARTESIAN_POINT('Ctrl Pts',(-23.534,10.4800654160338,2.48577456351454));
#207448=CARTESIAN_POINT('Ctrl Pts',(-23.534,10.3461486693946,2.46717850659781));
#207449=CARTESIAN_POINT('Ctrl Pts',(-23.534,10.211711690067,2.44851020870358));
#207450=CARTESIAN_POINT('Ctrl Pts',(-23.534,10.0762789980584,2.43582454854997));
#207451=CARTESIAN_POINT('Ctrl Pts',(-23.534,9.94025397646493,2.42915620857004));
#207452=CARTESIAN_POINT('Ctrl Pts',(-23.534,9.9245534826481,2.42838652495304));
#207453=CARTESIAN_POINT('Ctrl Pts',(-23.534,9.9088450894565,2.42769706425901));
#207454=CARTESIAN_POINT('Ctrl Pts',(-23.534,9.89312941238515,2.42708792441797));
#207455=CARTESIAN_POINT('Ctrl Pts',(-23.534,9.86982544152734,2.42618466221429));
#207456=CARTESIAN_POINT('Ctrl Pts',(-23.534,9.84650207816375,2.425458012161));
#207457=CARTESIAN_POINT('Ctrl Pts',(-23.534,9.82318746608169,2.4249087042635));
#207458=CARTESIAN_POINT('Ctrl Pts',(-23.534,9.68481926730006,2.42164865669821));
#207459=CARTESIAN_POINT('Ctrl Pts',(-23.534,9.54658084862216,2.42462233472131));
#207460=CARTESIAN_POINT('Ctrl Pts',(-23.534,9.40891306409928,2.43376529968542));
#207461=CARTESIAN_POINT('Ctrl Pts',(-23.534,9.26969699145749,2.44301109149514));
#207462=CARTESIAN_POINT('Ctrl Pts',(-23.534,9.13106368655266,2.45856549918087));
#207463=CARTESIAN_POINT('Ctrl Pts',(-23.534,8.99345056596637,2.48041133998068));
#207464=CARTESIAN_POINT('Ctrl Pts',(-23.534,8.97031116334576,2.48408467943915));
#207465=CARTESIAN_POINT('Ctrl Pts',(-23.534,8.94720057917996,2.48793601825196));
#207466=CARTESIAN_POINT('Ctrl Pts',(-23.534,8.9241208670849,2.49196541689415));
#207467=CARTESIAN_POINT('Ctrl Pts',(-23.534,8.7873871274078,2.51583723742324));
#207468=CARTESIAN_POINT('Ctrl Pts',(-23.534,8.65173684163142,2.54595438851018));
#207469=CARTESIAN_POINT('Ctrl Pts',(-23.534,8.51752579699816,2.58210352084366));
#207470=CARTESIAN_POINT('Ctrl Pts',(-23.534,8.39200772104798,2.61591124173701));
#207471=CARTESIAN_POINT('Ctrl Pts',(-23.534,8.2677479659076,2.65499549928287));
#207472=CARTESIAN_POINT('Ctrl Pts',(-23.534,8.14504361020047,2.69922256987843));
#207473=CARTESIAN_POINT('Ctrl Pts',(-23.534,8.12749669976606,2.70554710857997));
#207474=CARTESIAN_POINT('Ctrl Pts',(-23.534,8.10998161428438,2.71197687835703));
#207475=CARTESIAN_POINT('Ctrl Pts',(-23.534,8.09249924250724,2.71851155108686));
#207476=CARTESIAN_POINT('Ctrl Pts',(-23.534,8.07453683582073,2.72522565433514));
#207477=CARTESIAN_POINT('Ctrl Pts',(-23.534,8.05661738961167,2.73204736693228));
#207478=CARTESIAN_POINT('Ctrl Pts',(-23.534,8.03874521119562,2.73897465977803));
#207479=CARTESIAN_POINT('Ctrl Pts',(-23.534,7.90644077728778,2.79025612850192));
#207480=CARTESIAN_POINT('Ctrl Pts',(-23.534,7.77666647852651,2.84734176999563));
#207481=CARTESIAN_POINT('Ctrl Pts',(-23.534,7.64978171058127,2.90995636965286));
#207482=CARTESIAN_POINT('Ctrl Pts',(-23.534,7.52165755881585,2.97318257559647));
#207483=CARTESIAN_POINT('Ctrl Pts',(-23.534,7.39647891359876,3.04204645156364));
#207484=CARTESIAN_POINT('Ctrl Pts',(-23.534,7.27461872478453,3.11631789506347));
#207485=CARTESIAN_POINT('Ctrl Pts',(-23.534,7.15263517659778,3.19066452373046));
#207486=CARTESIAN_POINT('Ctrl Pts',(-23.534,7.03397603470935,3.27042992499855));
#207487=CARTESIAN_POINT('Ctrl Pts',(-23.534,6.91902974171529,3.35543308857631));
#207488=CARTESIAN_POINT('Ctrl Pts',(-23.534,6.88443823547605,3.38101362176852));
#207489=CARTESIAN_POINT('Ctrl Pts',(-23.534,6.8501831168222,3.40706882773967));
#207490=CARTESIAN_POINT('Ctrl Pts',(-23.534,6.81627539023442,3.43359460199418));
#207491=CARTESIAN_POINT('Ctrl Pts',(-23.534,6.76396915960913,3.47451339559359));
#207492=CARTESIAN_POINT('Ctrl Pts',(-23.534,6.71248951985117,3.51655187486385));
#207493=CARTESIAN_POINT('Ctrl Pts',(-23.534,6.66185982789806,3.55967699429164));
#207494=CARTESIAN_POINT('Ctrl Pts',(-23.534,6.63093354883434,3.58601923392675));
#207495=CARTESIAN_POINT('Ctrl Pts',(-23.534,6.60032442690432,3.6127669567928));
#207496=CARTESIAN_POINT('Ctrl Pts',(-23.534,6.5700380650519,3.63991298274907));
#207497=CARTESIAN_POINT('Ctrl Pts',(-23.534,6.54970174956393,3.65814066393382));
#207498=CARTESIAN_POINT('Ctrl Pts',(-23.534,6.52950985990992,3.67654895545334));
#207499=CARTESIAN_POINT('Ctrl Pts',(-23.534,6.50946759143304,3.69513255183675));
#207500=CARTESIAN_POINT('Ctrl Pts',(-23.534,6.48629939502987,3.71661457176801));
#207501=CARTESIAN_POINT('Ctrl Pts',(-23.534,6.46334194239172,3.73832084933172));
#207502=CARTESIAN_POINT('Ctrl Pts',(-23.534,6.44060381900491,3.76024083524255));
#207503=CARTESIAN_POINT('Ctrl Pts',(-23.534,6.33630358435424,3.86078825664344));
#207504=CARTESIAN_POINT('Ctrl Pts',(-23.534,6.23656911765673,3.96587231787068));
#207505=CARTESIAN_POINT('Ctrl Pts',(-23.534,6.14160415274189,4.07509691465864));
#207506=CARTESIAN_POINT('Ctrl Pts',(-23.534,6.04554420146357,4.18558091741959));
#207507=CARTESIAN_POINT('Ctrl Pts',(-23.534,5.9543637852261,4.30030196798446));
#207508=CARTESIAN_POINT('Ctrl Pts',(-23.534,5.86830289292554,4.41889447763156));
#207509=CARTESIAN_POINT('Ctrl Pts',(-23.534,5.82757976357167,4.47501123382195));
#207510=CARTESIAN_POINT('Ctrl Pts',(-23.534,5.78800341363274,4.53199543604809));
#207511=CARTESIAN_POINT('Ctrl Pts',(-23.534,5.74960209595384,4.58981127009334));
#207512=CARTESIAN_POINT('Ctrl Pts',(-23.534,5.73602768423563,4.61024848377764));
#207513=CARTESIAN_POINT('Ctrl Pts',(-23.534,5.72260309324962,4.63078521650428));
#207514=CARTESIAN_POINT('Ctrl Pts',(-23.534,5.7093336961382,4.65141296650499));
#207515=CARTESIAN_POINT('Ctrl Pts',(-23.534,5.62878693151662,4.77662577836291));
#207516=CARTESIAN_POINT('Ctrl Pts',(-23.534,5.55390603885587,4.90526364111019));
#207517=CARTESIAN_POINT('Ctrl Pts',(-23.534,5.48492211365496,5.03693496093977));
#207518=CARTESIAN_POINT('Ctrl Pts',(-23.534,5.43386982584413,5.13437972211847));
#207519=CARTESIAN_POINT('Ctrl Pts',(-23.534,5.38604780954608,5.23348685196463));
#207520=CARTESIAN_POINT('Ctrl Pts',(-23.534,5.34156275575684,5.33411058694693));
#207521=CARTESIAN_POINT('Ctrl Pts',(-23.534,5.29184265751413,5.4465758210584));
#207522=CARTESIAN_POINT('Ctrl Pts',(-23.534,5.24629059068216,5.56093558465364));
#207523=CARTESIAN_POINT('Ctrl Pts',(-23.534,5.20492644341908,5.67694766332001));
#207524=CARTESIAN_POINT('Ctrl Pts',(-23.5319822466055,5.20171862064502,
8.32379167009335));
#207525=CARTESIAN_POINT('Ctrl Pts',(-23.4932003649694,5.41676747330397,
9.12430564500732));
#207526=CARTESIAN_POINT('Ctrl Pts',(-23.4156366016973,6.24411030078641,
10.617835827178));
#207527=CARTESIAN_POINT('Ctrl Pts',(-23.2992909567891,8.39090024522478,
12.0161880404286));
#207528=CARTESIAN_POINT('Ctrl Pts',(-23.1829453118809,10.9421734655344,
12.2463212707424));
#207529=CARTESIAN_POINT('Ctrl Pts',(-23.0665996669727,13.304392578115,11.2549883803824));
#207530=CARTESIAN_POINT('Ctrl Pts',(-22.9502540220645,14.927276862139,9.2728561879833));
#207531=CARTESIAN_POINT('Ctrl Pts',(-22.8339083771563,15.4330671204992,
6.7615280730017));
#207532=CARTESIAN_POINT('Ctrl Pts',(-22.7175627322481,14.7039361435109,
4.30571495106923));
#207533=CARTESIAN_POINT('Ctrl Pts',(-22.6012170873399,12.9096846230479,
2.47725497604962));
#207534=CARTESIAN_POINT('Ctrl Pts',(-22.4848714424317,10.4680804717197,
1.70188576751079));
#207535=CARTESIAN_POINT('Ctrl Pts',(-22.3685257975235,7.94764111846411,
2.16015054073166));
#207536=CARTESIAN_POINT('Ctrl Pts',(-22.2521801526153,5.93523494026475,
3.74534471809911));
#207537=CARTESIAN_POINT('Ctrl Pts',(-22.1358345077071,4.89943419990334,
6.08836351785797));
#207538=CARTESIAN_POINT('Ctrl Pts',(-22.0194888627989,5.08142954165806,
8.64365537460478));
#207539=CARTESIAN_POINT('Ctrl Pts',(-21.9031432178907,6.43882069342724,
10.8162233567271));
#207540=CARTESIAN_POINT('Ctrl Pts',(-21.7867975729826,8.65559778633532,
12.1002259870008));
#207541=CARTESIAN_POINT('Ctrl Pts',(-21.6704519280743,11.2154925541789,
12.1966333884833));
#207542=CARTESIAN_POINT('Ctrl Pts',(-21.5541062831661,13.5226699559939,
11.0831186756717));
#207543=CARTESIAN_POINT('Ctrl Pts',(-21.4377606382579,15.0394563872939,
9.01870375488018));
#207544=CARTESIAN_POINT('Ctrl Pts',(-21.3214149933497,15.4136431368683,
6.48460438397758));
#207545=CARTESIAN_POINT('Ctrl Pts',(-21.2050693484416,14.5560831704402,
4.06976232245845));
#207546=CARTESIAN_POINT('Ctrl Pts',(-21.0887237035334,12.6706797211637,
2.33877575209256));
#207547=CARTESIAN_POINT('Ctrl Pts',(-20.9723780586252,10.1876014272064,
1.68985066266665));
#207548=CARTESIAN_POINT('Ctrl Pts',(-20.856032413717,7.70350655415105,2.28420940052766));
#207549=CARTESIAN_POINT('Ctrl Pts',(-20.7009048871727,5.11052082316887,
4.5226382644136));
#207550=CARTESIAN_POINT('Ctrl Pts',(-20.5069954789924,4.53607622899261,
9.14006197037595));
#207551=CARTESIAN_POINT('Ctrl Pts',(-20.274304189176,8.77988224509149,12.8347910532216));
#207552=CARTESIAN_POINT('Ctrl Pts',(-20.0803947809957,13.2742515855875,
11.6301199348782));
#207553=CARTESIAN_POINT('Ctrl Pts',(-19.9252672544514,15.1343801571744,
8.75365326951933));
#207554=CARTESIAN_POINT('Ctrl Pts',(-19.8089216095432,15.3810853499648,
6.21138534590041));
#207555=CARTESIAN_POINT('Ctrl Pts',(-19.692575964635,14.3964856232887,3.84129147353207));
#207556=CARTESIAN_POINT('Ctrl Pts',(-19.5762303197268,12.4224121035996,
2.21215231060185));
#207557=CARTESIAN_POINT('Ctrl Pts',(-19.4598846748187,9.91250172714882,
1.69521790442747));
#207558=CARTESIAN_POINT('Ctrl Pts',(-19.3435390299104,7.45404844673223,
2.4147196856449));
#207559=CARTESIAN_POINT('Ctrl Pts',(-19.2271933850022,5.6181127491502,4.20127787325212));
#207560=CARTESIAN_POINT('Ctrl Pts',(-19.110847740094,4.83283831742701,6.63978697636726));
#207561=CARTESIAN_POINT('Ctrl Pts',(-18.9945020951859,5.28075719645332,
9.16203285797858));
#207562=CARTESIAN_POINT('Ctrl Pts',(-18.8781564502777,6.85772444914764,
11.1809280306217));
#207563=CARTESIAN_POINT('Ctrl Pts',(-18.7618108053695,9.19648123363852,
12.2262887716303));
#207564=CARTESIAN_POINT('Ctrl Pts',(-18.6454651604612,11.7524966959059,
12.054755293186));
#207565=CARTESIAN_POINT('Ctrl Pts',(-18.5291195155531,13.9306022671102,
10.7062463423646));
#207566=CARTESIAN_POINT('Ctrl Pts',(-18.4127738706449,15.2236468447518,
8.49476382462988));
#207567=CARTESIAN_POINT('Ctrl Pts',(-18.2964282257367,15.3305503344285,
5.93523402802474));
#207568=CARTESIAN_POINT('Ctrl Pts',(-18.1800825808285,14.2264204181411,
3.62362736397207));
#207569=CARTESIAN_POINT('Ctrl Pts',(-18.0637369359203,12.1683508661136,
2.09819164983995));
#207570=CARTESIAN_POINT('Ctrl Pts',(-17.9473912910121,9.63554082881353,
1.71410391713887));
#207571=CARTESIAN_POINT('Ctrl Pts',(-17.8310456461039,7.21776027584542,
2.56082103887325));
#207572=CARTESIAN_POINT('Ctrl Pts',(-17.7147000011957,5.47793063941487,
4.44113863536456));
#207573=CARTESIAN_POINT('Ctrl Pts',(-17.5983543562875,4.82125235646171,
6.91734413330858));
#207574=CARTESIAN_POINT('Ctrl Pts',(-17.4820087113793,5.40043672555636,
9.41264007065955));
#207575=CARTESIAN_POINT('Ctrl Pts',(-17.365659185369,7.08108537827514,11.3465361450299));
#207576=CARTESIAN_POINT('Ctrl Pts',(-17.2880915409948,8.67440018888338,
11.9603782381559));
#207577=CARTESIAN_POINT('Ctrl Pts',(-17.2493057782566,9.49698541727643,
12.0631392445802));
#207578=CARTESIAN_POINT('Ctrl Pts',(-23.6945707061519,5.47368749304882,
8.25073036722769));
#207579=CARTESIAN_POINT('Ctrl Pts',(-23.6557888245159,5.67686759799619,
9.00706322566336));
#207580=CARTESIAN_POINT('Ctrl Pts',(-23.5782250612437,6.45854859948439,
10.4181640774162));
#207581=CARTESIAN_POINT('Ctrl Pts',(-23.4618794163355,8.48685519502201,
11.7393399215497));
#207582=CARTESIAN_POINT('Ctrl Pts',(-23.3455337714274,10.8973212553735,
11.9567718832129));
#207583=CARTESIAN_POINT('Ctrl Pts',(-23.2291881265191,13.1291672813738,
11.0201515841008));
#207584=CARTESIAN_POINT('Ctrl Pts',(-23.112842481611,14.6624830608743,9.14741512495814));
#207585=CARTESIAN_POINT('Ctrl Pts',(-22.9964968367027,15.1403582808735,
6.77468956213704));
#207586=CARTESIAN_POINT('Ctrl Pts',(-22.8801511917946,14.4514687258114,
4.45441506787272));
#207587=CARTESIAN_POINT('Ctrl Pts',(-22.7638055468864,12.7562436282479,
2.72686951241825));
#207588=CARTESIAN_POINT('Ctrl Pts',(-22.6474599019782,10.4493938981843,
1.99429365713702));
#207589=CARTESIAN_POINT('Ctrl Pts',(-22.53111425707,8.06805995486816,2.42726636806037));
#207590=CARTESIAN_POINT('Ctrl Pts',(-22.4147686121618,6.1667203595729,3.92497219321195));
#207591=CARTESIAN_POINT('Ctrl Pts',(-22.2984229672536,5.18808643277415,
6.13867758964879));
#207592=CARTESIAN_POINT('Ctrl Pts',(-22.1820773223454,5.36003728106023,
8.55294049412641));
#207593=CARTESIAN_POINT('Ctrl Pts',(-22.0657316774372,6.64251274308225,
10.6056024132903));
#207594=CARTESIAN_POINT('Ctrl Pts',(-21.949386032529,8.73694383077701,11.8187397350944));
#207595=CARTESIAN_POINT('Ctrl Pts',(-21.8330403876208,11.1555556073744,
11.9098263217407));
#207596=CARTESIAN_POINT('Ctrl Pts',(-21.7166947427126,13.3353977262086,
10.857767529461));
#207597=CARTESIAN_POINT('Ctrl Pts',(-21.6003490978044,14.7684712929067,
8.90728960281731));
#207598=CARTESIAN_POINT('Ctrl Pts',(-21.4840034528962,15.1220063251024,
6.51304955102958));
#207599=CARTESIAN_POINT('Ctrl Pts',(-21.367657807988,14.311775896885,4.23148488595831));
#207600=CARTESIAN_POINT('Ctrl Pts',(-21.2513121630798,12.5304296308826,
2.59603308660738));
#207601=CARTESIAN_POINT('Ctrl Pts',(-21.1349665181716,10.184394754989,1.98292278100795));
#207602=CARTESIAN_POINT('Ctrl Pts',(-21.0186208732634,7.83739940595061,
2.54447830312228));
#207603=CARTESIAN_POINT('Ctrl Pts',(-20.8634933467192,5.38752298748152,
4.65936618026363));
#207604=CARTESIAN_POINT('Ctrl Pts',(-20.6695839385389,4.84478252879942,
9.02194994466884));
#207605=CARTESIAN_POINT('Ctrl Pts',(-20.4368926487225,8.85436891378104,
12.5127634669118));
#207606=CARTESIAN_POINT('Ctrl Pts',(-20.2429832405422,13.1006897984706,
11.374579276549));
#207607=CARTESIAN_POINT('Ctrl Pts',(-20.0878557139979,14.8581561309695,
8.65686750213595));
#207608=CARTESIAN_POINT('Ctrl Pts',(-19.9715100690897,15.0912454329697,
6.25490972771149));
#207609=CARTESIAN_POINT('Ctrl Pts',(-19.8551644241815,14.1609866879279,
4.01562355729595));
#207610=CARTESIAN_POINT('Ctrl Pts',(-19.7388187792733,12.2958641357962,
2.47639811151788));
#207611=CARTESIAN_POINT('Ctrl Pts',(-19.6224731343651,9.92447806518769,
1.98799379966607));
#207612=CARTESIAN_POINT('Ctrl Pts',(-19.5061274894569,7.60170912526025,
2.66778560329601));
#207613=CARTESIAN_POINT('Ctrl Pts',(-19.3897818445487,5.86710043937747,
4.35574197025367));
#207614=CARTESIAN_POINT('Ctrl Pts',(-19.2734361996405,5.12516603946211,
6.65966747071569));
#207615=CARTESIAN_POINT('Ctrl Pts',(-19.1570905547323,5.54836385578716,
9.04270823839462));
#207616=CARTESIAN_POINT('Ctrl Pts',(-19.0407449098241,7.0382968079482,10.9501786944492));
#207617=CARTESIAN_POINT('Ctrl Pts',(-18.9243992649159,9.24797541373385,
11.9378449965002));
#207618=CARTESIAN_POINT('Ctrl Pts',(-18.8080536200077,11.6629219872652,
11.775778611484));
#207619=CARTESIAN_POINT('Ctrl Pts',(-18.6917079750996,13.7208158707802,
10.5016951334156));
#207620=CARTESIAN_POINT('Ctrl Pts',(-18.5753623301913,14.9424961064032,
8.41226640832857));
#207621=CARTESIAN_POINT('Ctrl Pts',(-18.4590166852832,15.0434994922998,
5.99399945986498));
#207622=CARTESIAN_POINT('Ctrl Pts',(-18.342671040375,14.0003075408293,3.80997253392679));
#207623=CARTESIAN_POINT('Ctrl Pts',(-18.2263253954668,12.0558247761009,
2.36872704642182));
#207624=CARTESIAN_POINT('Ctrl Pts',(-18.1099797505586,9.66280289838584,
2.00583747563687));
#207625=CARTESIAN_POINT('Ctrl Pts',(-17.9936341056504,7.37846191996246,
2.8058234859206));
#207626=CARTESIAN_POINT('Ctrl Pts',(-17.8772884607422,5.73465511165029,
4.58236459211928));
#207627=CARTESIAN_POINT('Ctrl Pts',(-17.760942815834,5.11421951854028,6.92190598805235));
#207628=CARTESIAN_POINT('Ctrl Pts',(-17.6445971709258,5.66143815952116,
9.27948420415084));
#207629=CARTESIAN_POINT('Ctrl Pts',(-17.5282476449155,7.24933023807416,
11.1066467418232));
#207630=CARTESIAN_POINT('Ctrl Pts',(-17.4506800005413,8.75470851110772,
11.6866103145668));
#207631=CARTESIAN_POINT('Ctrl Pts',(-17.411894237803,9.53189448985888,11.7836998447437));
#207632=CARTESIAN_POINT('Ctrl Pts',(-23.8571591656983,5.74565636545262,
8.17766906436202));
#207633=CARTESIAN_POINT('Ctrl Pts',(-23.8183772840622,5.93696772268841,
8.88982080631942));
#207634=CARTESIAN_POINT('Ctrl Pts',(-23.7408135207901,6.67298689818237,
10.2184923276544));
#207635=CARTESIAN_POINT('Ctrl Pts',(-23.6244678758819,8.58281014481923,
11.4624918026709));
#207636=CARTESIAN_POINT('Ctrl Pts',(-23.5081222309737,10.8524690452125,
11.6672224956832));
#207637=CARTESIAN_POINT('Ctrl Pts',(-23.3917765860655,12.9539419846326,
10.7853147878191));
#207638=CARTESIAN_POINT('Ctrl Pts',(-23.2754309411573,14.3976892596095,
9.021974061933));
#207639=CARTESIAN_POINT('Ctrl Pts',(-23.1590852962491,14.8476494412477,
6.78785105127238));
#207640=CARTESIAN_POINT('Ctrl Pts',(-23.0427396513409,14.1990013081117,
4.6031151846762));
#207641=CARTESIAN_POINT('Ctrl Pts',(-22.9263940064328,12.6028026334481,
2.97648404878689));
#207642=CARTESIAN_POINT('Ctrl Pts',(-22.8100483615245,10.4307073246489,
2.28670154676325));
#207643=CARTESIAN_POINT('Ctrl Pts',(-22.6937027166164,8.18847879127224,
2.69438219538906));
#207644=CARTESIAN_POINT('Ctrl Pts',(-22.5773570717082,6.39820577888104,
4.10459966832482));
#207645=CARTESIAN_POINT('Ctrl Pts',(-22.4610114268,5.47673866564495,6.18899166143961));
#207646=CARTESIAN_POINT('Ctrl Pts',(-22.3446657818918,5.6386450204624,8.46222561364805));
#207647=CARTESIAN_POINT('Ctrl Pts',(-22.2283201369836,6.84620479273727,
10.3949814698534));
#207648=CARTESIAN_POINT('Ctrl Pts',(-22.1119744920754,8.81828987521867,
11.5372534831879));
#207649=CARTESIAN_POINT('Ctrl Pts',(-21.9956288471672,11.0956186605698,
11.6230192549981));
#207650=CARTESIAN_POINT('Ctrl Pts',(-21.879283202259,13.1481254964233,10.6324163832503));
#207651=CARTESIAN_POINT('Ctrl Pts',(-21.7629375573508,14.4974861985194,
8.79587545075443));
#207652=CARTESIAN_POINT('Ctrl Pts',(-21.6465919124426,14.8303695133365,
6.54149471808157));
#207653=CARTESIAN_POINT('Ctrl Pts',(-21.5302462675344,14.0674686233298,
4.39320744945815));
#207654=CARTESIAN_POINT('Ctrl Pts',(-21.4139006226262,12.3901795406013,
2.8532904211222));
#207655=CARTESIAN_POINT('Ctrl Pts',(-21.297554977718,10.1811880827716,2.27599489934924));
#207656=CARTESIAN_POINT('Ctrl Pts',(-21.1812093328098,7.97129225775015,
2.80474720571691));
#207657=CARTESIAN_POINT('Ctrl Pts',(-21.0260818062656,5.66452515179418,
4.79609409611365));
#207658=CARTESIAN_POINT('Ctrl Pts',(-20.8321723980852,5.1534888286062,8.90383791896172));
#207659=CARTESIAN_POINT('Ctrl Pts',(-20.5994811082689,8.92885558247061,
12.1907358806019));
#207660=CARTESIAN_POINT('Ctrl Pts',(-20.4055717000885,12.9271280113536,
11.1190386182196));
#207661=CARTESIAN_POINT('Ctrl Pts',(-20.2504441735443,14.5819321047646,
8.56008173475257));
#207662=CARTESIAN_POINT('Ctrl Pts',(-20.1340985286361,14.8014055159746,
6.29843410952257));
#207663=CARTESIAN_POINT('Ctrl Pts',(-20.0177528837279,13.925487752567,4.18995564105982));
#207664=CARTESIAN_POINT('Ctrl Pts',(-19.9014072388197,12.1693161679927,
2.74064391243392));
#207665=CARTESIAN_POINT('Ctrl Pts',(-19.7850615939115,9.93645440322659,
2.28076969490466));
#207666=CARTESIAN_POINT('Ctrl Pts',(-19.6687159490033,7.74936980378826,
2.92085152094712));
#207667=CARTESIAN_POINT('Ctrl Pts',(-19.5523703040951,6.11608812960472,
4.51020606725524));
#207668=CARTESIAN_POINT('Ctrl Pts',(-19.4360246591869,5.41749376149721,
6.67954796506412));
#207669=CARTESIAN_POINT('Ctrl Pts',(-19.3196790142787,5.81597051512098,
8.92338361881067));
#207670=CARTESIAN_POINT('Ctrl Pts',(-19.2033333693705,7.21886916674878,
10.7194293582766));
#207671=CARTESIAN_POINT('Ctrl Pts',(-19.0869877244623,9.29946959382919,
11.6494012213701));
#207672=CARTESIAN_POINT('Ctrl Pts',(-18.9706420795541,11.5733472786245,
11.4968019297822));
#207673=CARTESIAN_POINT('Ctrl Pts',(-18.8542964346459,13.51102947445,10.2971439244665));
#207674=CARTESIAN_POINT('Ctrl Pts',(-18.7379507897377,14.6613453680545,
8.32976899202724));
#207675=CARTESIAN_POINT('Ctrl Pts',(-18.6216051448295,14.756448650171,6.05276489170521));
#207676=CARTESIAN_POINT('Ctrl Pts',(-18.5052594999214,13.7741946635174,
3.9963177038815));
#207677=CARTESIAN_POINT('Ctrl Pts',(-18.3889138550131,11.9432986860881,
2.6392624430037));
#207678=CARTESIAN_POINT('Ctrl Pts',(-18.272568210105,9.69006496795816,2.29757103413487));
#207679=CARTESIAN_POINT('Ctrl Pts',(-18.1562225651967,7.5391635640795,3.05082593296795));
#207680=CARTESIAN_POINT('Ctrl Pts',(-18.0398769202886,5.9913795838857,4.72359054887402));
#207681=CARTESIAN_POINT('Ctrl Pts',(-17.9235312753804,5.40718668061885,
6.9264678427961));
#207682=CARTESIAN_POINT('Ctrl Pts',(-17.8071856304722,5.92243959348596,
9.14632833764213));
#207683=CARTESIAN_POINT('Ctrl Pts',(-17.6908361044619,7.41757509787318,
10.8667573386166));
#207684=CARTESIAN_POINT('Ctrl Pts',(-17.6132684600876,8.83501683333207,
11.4128423909775));
#207685=CARTESIAN_POINT('Ctrl Pts',(-17.5744826973495,9.56680356244131,
11.5042604449073));
#207686=CARTESIAN_POINT('Ctrl Pts',(-24.0197476252447,6.01762523785643,
8.10460776149636));
#207687=CARTESIAN_POINT('Ctrl Pts',(-23.9809657436086,6.19706784738064,
8.77257838697545));
#207688=CARTESIAN_POINT('Ctrl Pts',(-23.9034019803365,6.88742519688036,
10.0188205778924));
#207689=CARTESIAN_POINT('Ctrl Pts',(-23.7870563354283,8.67876509461647,
11.185643683792));
#207690=CARTESIAN_POINT('Ctrl Pts',(-23.6707106905201,10.8076168350517,
11.3776731081537));
#207691=CARTESIAN_POINT('Ctrl Pts',(-23.5543650456119,12.7787166878914,
10.5504779915376));
#207692=CARTESIAN_POINT('Ctrl Pts',(-23.4380194007037,14.1328954583448,
8.89653299890785));
#207693=CARTESIAN_POINT('Ctrl Pts',(-23.3216737557955,14.5549406016221,
6.80101254040771));
#207694=CARTESIAN_POINT('Ctrl Pts',(-23.2053281108873,13.9465338904122,
4.75181530147969));
#207695=CARTESIAN_POINT('Ctrl Pts',(-23.0889824659791,12.4493616386481,
3.22609858515552));
#207696=CARTESIAN_POINT('Ctrl Pts',(-22.9726368210709,10.4120207511136,
2.57910943638948));
#207697=CARTESIAN_POINT('Ctrl Pts',(-22.8562911761627,8.30889762767629,
2.96149802271777));
#207698=CARTESIAN_POINT('Ctrl Pts',(-22.7399455312545,6.62969119818919,
4.28422714343766));
#207699=CARTESIAN_POINT('Ctrl Pts',(-22.6235998863464,5.76539089851575,
6.23930573323043));
#207700=CARTESIAN_POINT('Ctrl Pts',(-22.5072542414381,5.91725275986458,
8.37151073316967));
#207701=CARTESIAN_POINT('Ctrl Pts',(-22.39090859653,7.04989684239228,10.1843605264167));
#207702=CARTESIAN_POINT('Ctrl Pts',(-22.2745629516218,8.89963591966034,
11.2557672312814));
#207703=CARTESIAN_POINT('Ctrl Pts',(-22.1582173067136,11.0356817137652,
11.3362121882554));
#207704=CARTESIAN_POINT('Ctrl Pts',(-22.0418716618054,12.9608532666381,
10.4070652370397));
#207705=CARTESIAN_POINT('Ctrl Pts',(-21.9255260168972,14.2265011041321,
8.68446129869154));
#207706=CARTESIAN_POINT('Ctrl Pts',(-21.809180371989,14.5387327015706,6.56993988513358));
#207707=CARTESIAN_POINT('Ctrl Pts',(-21.6928347270808,13.8231613497746,
4.554930012958));
#207708=CARTESIAN_POINT('Ctrl Pts',(-21.5764890821726,12.2499294503202,
3.11054775563703));
#207709=CARTESIAN_POINT('Ctrl Pts',(-21.4601434372644,10.1779814105543,
2.56906701769053));
#207710=CARTESIAN_POINT('Ctrl Pts',(-21.3437977923562,8.10518510954971,
3.06501610831153));
#207711=CARTESIAN_POINT('Ctrl Pts',(-21.1886702658119,5.94152731610683,
4.93282201196367));
#207712=CARTESIAN_POINT('Ctrl Pts',(-20.9947608576316,5.462195128413,8.78572589325462));
#207713=CARTESIAN_POINT('Ctrl Pts',(-20.7620695678152,9.00334225116017,
11.868708294292));
#207714=CARTESIAN_POINT('Ctrl Pts',(-20.5681601596349,12.7535662242368,
10.8634979598904));
#207715=CARTESIAN_POINT('Ctrl Pts',(-20.4130326330907,14.3057080785598,
8.46329596736919));
#207716=CARTESIAN_POINT('Ctrl Pts',(-20.2966869881824,14.5115655989794,
6.34195849133365));
#207717=CARTESIAN_POINT('Ctrl Pts',(-20.1803413432743,13.6899888172062,
4.3642877248237));
#207718=CARTESIAN_POINT('Ctrl Pts',(-20.063995698366,12.0427682001893,3.00488971334995));
#207719=CARTESIAN_POINT('Ctrl Pts',(-19.9476500534579,9.94843074126549,
2.57354559014325));
#207720=CARTESIAN_POINT('Ctrl Pts',(-19.8313044085497,7.89703048231626,
3.17391743859823));
#207721=CARTESIAN_POINT('Ctrl Pts',(-19.7149587636415,6.36507581983199,
4.66467016425681));
#207722=CARTESIAN_POINT('Ctrl Pts',(-19.5986131187333,5.7098214835323,6.69942845941255));
#207723=CARTESIAN_POINT('Ctrl Pts',(-19.4822674738251,6.08357717445482,
8.80405899922673));
#207724=CARTESIAN_POINT('Ctrl Pts',(-19.3659218289169,7.39944152554934,
10.4886800221041));
#207725=CARTESIAN_POINT('Ctrl Pts',(-19.2495761840087,9.35096377392451,
11.36095744624));
#207726=CARTESIAN_POINT('Ctrl Pts',(-19.1332305391005,11.4837725699839,
11.2178252480802));
#207727=CARTESIAN_POINT('Ctrl Pts',(-19.0168848941923,13.3012430781199,
10.0925927155175));
#207728=CARTESIAN_POINT('Ctrl Pts',(-18.9005392492841,14.3801946297058,
8.2472715757259));
#207729=CARTESIAN_POINT('Ctrl Pts',(-18.7841936043759,14.4693978080423,
6.11153032354543));
#207730=CARTESIAN_POINT('Ctrl Pts',(-18.6678479594677,13.5480817862055,
4.18266287383621));
#207731=CARTESIAN_POINT('Ctrl Pts',(-18.5515023145595,11.8307725960754,
2.90979783958556));
#207732=CARTESIAN_POINT('Ctrl Pts',(-18.4351566696513,9.71732703753046,
2.58930459263287));
#207733=CARTESIAN_POINT('Ctrl Pts',(-18.3188110247431,7.69986520819653,
3.29582838001529));
#207734=CARTESIAN_POINT('Ctrl Pts',(-18.2024653798349,6.24810405612113,
4.86481650562875));
#207735=CARTESIAN_POINT('Ctrl Pts',(-18.0861197349267,5.70015384269742,
6.93102969753986));
#207736=CARTESIAN_POINT('Ctrl Pts',(-17.9697740900186,6.18344102745076,
9.01317247113341));
#207737=CARTESIAN_POINT('Ctrl Pts',(-17.8534245640082,7.58581995767219,
10.6268679354101));
#207738=CARTESIAN_POINT('Ctrl Pts',(-17.775856919634,8.91532515555641,11.1390744673883));
#207739=CARTESIAN_POINT('Ctrl Pts',(-17.7370711568959,9.60171263502375,
11.2248210450709));
#207740=CARTESIAN_POINT('Ctrl Pts',(-17.734,9.60084442449481,11.2300936493755));
#207741=CARTESIAN_POINT('Ctrl Pts',(-17.734,9.47184184893842,11.2265276083404));
#207742=CARTESIAN_POINT('Ctrl Pts',(-17.734,9.34319367231557,11.2169788959015));
#207743=CARTESIAN_POINT('Ctrl Pts',(-17.734,9.21527281511507,11.2016549822556));
#207744=CARTESIAN_POINT('Ctrl Pts',(-17.734,9.0850114707997,11.1860506966421));
#207745=CARTESIAN_POINT('Ctrl Pts',(-17.734,8.95550358620178,11.1644579949205));
#207746=CARTESIAN_POINT('Ctrl Pts',(-17.7339999999999,8.82713205802554,
11.137043167845));
#207747=CARTESIAN_POINT('Ctrl Pts',(-17.7339999999999,8.77054626711207,
11.1249587929462));
#207748=CARTESIAN_POINT('Ctrl Pts',(-17.734,8.71418119819127,11.1117424824689));
#207749=CARTESIAN_POINT('Ctrl Pts',(-17.7339999999999,8.65806956321802,
11.0974052780753));
#207750=CARTESIAN_POINT('Ctrl Pts',(-17.7339999999999,8.63585998151805,
11.0917304601435));
#207751=CARTESIAN_POINT('Ctrl Pts',(-17.734,8.61369010565667,11.0858800148832));
#207752=CARTESIAN_POINT('Ctrl Pts',(-17.734,8.59156197215374,11.0798545436473));
#207753=CARTESIAN_POINT('Ctrl Pts',(-17.734,8.56803675576561,11.073448647974));
#207754=CARTESIAN_POINT('Ctrl Pts',(-17.734,8.54456657927922,11.0668470333961));
#207755=CARTESIAN_POINT('Ctrl Pts',(-17.734,8.52115967302967,11.0600525704303));
#207756=CARTESIAN_POINT('Ctrl Pts',(-17.734,8.39238352917026,11.0226719473357));
#207757=CARTESIAN_POINT('Ctrl Pts',(-17.7339999999999,8.2654669075248,10.9794433217256));
#207758=CARTESIAN_POINT('Ctrl Pts',(-17.7339999999999,8.14080691439627,
10.9305498903925));
#207759=CARTESIAN_POINT('Ctrl Pts',(-17.7339999999999,8.04196929345981,
10.8917843625668));
#207760=CARTESIAN_POINT('Ctrl Pts',(-17.7339999999999,7.94454991934812,
10.8494567334459));
#207761=CARTESIAN_POINT('Ctrl Pts',(-17.7339999999999,7.84874780521351,
10.8036350740797));
#207762=CARTESIAN_POINT('Ctrl Pts',(-17.7339999999999,7.8007073644388,10.780657577885));
#207763=CARTESIAN_POINT('Ctrl Pts',(-17.734,7.75307363883164,10.7568011656462));
#207764=CARTESIAN_POINT('Ctrl Pts',(-17.734,7.70587215411362,10.7320725309682));
#207765=CARTESIAN_POINT('Ctrl Pts',(-17.734,7.6793174922842,10.7181606691847));
#207766=CARTESIAN_POINT('Ctrl Pts',(-17.734,7.65289964014865,10.7039727286759));
#207767=CARTESIAN_POINT('Ctrl Pts',(-17.734,7.6266232029969,10.6895097288812));
#207768=CARTESIAN_POINT('Ctrl Pts',(-17.734,7.60953423118557,10.6801036669266));
#207769=CARTESIAN_POINT('Ctrl Pts',(-17.734,7.59250626485928,10.6705818595696));
#207770=CARTESIAN_POINT('Ctrl Pts',(-17.734,7.57555065957241,10.660950526036));
#207771=CARTESIAN_POINT('Ctrl Pts',(-17.734,7.57223521227194,10.6590672444767));
#207772=CARTESIAN_POINT('Ctrl Pts',(-17.734,7.56892242572952,10.6571797172604));
#207773=CARTESIAN_POINT('Ctrl Pts',(-17.734,7.56561230852364,10.655287949029));
#207774=CARTESIAN_POINT('Ctrl Pts',(-17.734,7.4452780447926,10.5865155995581));
#207775=CARTESIAN_POINT('Ctrl Pts',(-17.734,7.32847088871135,10.5121436774441));
#207776=CARTESIAN_POINT('Ctrl Pts',(-17.734,7.21544353549545,10.4326038138175));
#207777=CARTESIAN_POINT('Ctrl Pts',(-17.734,7.10471415648963,10.3546810857788));
#207778=CARTESIAN_POINT('Ctrl Pts',(-17.734,6.9976118719238,10.2717977527096));
#207779=CARTESIAN_POINT('Ctrl Pts',(-17.734,6.89438670712407,10.1843052779667));
#207780=CARTESIAN_POINT('Ctrl Pts',(-17.734,6.78794818419838,10.0940891974518));
#207781=CARTESIAN_POINT('Ctrl Pts',(-17.734,6.6856311233395,9.99897228946867));
#207782=CARTESIAN_POINT('Ctrl Pts',(-17.734,6.58773359226503,9.89928785076239));
#207783=CARTESIAN_POINT('Ctrl Pts',(-17.734,6.48983606119057,9.79960341205611));
#207784=CARTESIAN_POINT('Ctrl Pts',(-17.734,6.39635732386311,9.69535089177202));
#207785=CARTESIAN_POINT('Ctrl Pts',(-17.734,6.30763052920929,9.58681889811916));
#207786=CARTESIAN_POINT('Ctrl Pts',(-17.734,6.29613696047738,9.57275978628571));
#207787=CARTESIAN_POINT('Ctrl Pts',(-17.734,6.2847217875374,9.55862705010366));
#207788=CARTESIAN_POINT('Ctrl Pts',(-17.734,6.27339033844863,9.54442698291116));
#207789=CARTESIAN_POINT('Ctrl Pts',(-17.734,6.18608899588886,9.43502482960916));
#207790=CARTESIAN_POINT('Ctrl Pts',(-17.734,6.10395851094937,9.32188720168948));
#207791=CARTESIAN_POINT('Ctrl Pts',(-17.734,6.02725312841166,9.20538411899327));
#207792=CARTESIAN_POINT('Ctrl Pts',(-17.734,6.00879365458167,9.17734716076432));
#207793=CARTESIAN_POINT('Ctrl Pts',(-17.734,5.99064847657934,9.14911508036603));
#207794=CARTESIAN_POINT('Ctrl Pts',(-17.734,5.97282135213961,9.12069264219457));
#207795=CARTESIAN_POINT('Ctrl Pts',(-17.734,5.89932193605749,9.00350982809041));
#207796=CARTESIAN_POINT('Ctrl Pts',(-17.734,5.83122601110488,8.88309435288582));
#207797=CARTESIAN_POINT('Ctrl Pts',(-17.734,5.76858202624982,8.75987299061834));
#207798=CARTESIAN_POINT('Ctrl Pts',(-17.734,5.70371974075208,8.63228820817982));
#207799=CARTESIAN_POINT('Ctrl Pts',(-17.734,5.64470175837658,8.5016947685322));
#207800=CARTESIAN_POINT('Ctrl Pts',(-17.734,5.59162577020732,8.36852853807731));
#207801=CARTESIAN_POINT('Ctrl Pts',(-17.734,5.53854978203807,8.23536230762243));
#207802=CARTESIAN_POINT('Ctrl Pts',(-17.734,5.49141540954945,8.099622483443));
#207803=CARTESIAN_POINT('Ctrl Pts',(-17.734,5.45037050417322,7.96171819969766));
#207804=CARTESIAN_POINT('Ctrl Pts',(-17.734,5.44370883977346,7.93933607823385));
#207805=CARTESIAN_POINT('Ctrl Pts',(-17.734,5.43720810246527,7.91689789292579));
#207806=CARTESIAN_POINT('Ctrl Pts',(-17.734,5.43087453784511,7.89442611014828));
#207807=CARTESIAN_POINT('Ctrl Pts',(-17.734,5.39210005999986,7.75685245365212));
#207808=CARTESIAN_POINT('Ctrl Pts',(-17.734,5.35952760979182,7.61782263160567));
#207809=CARTESIAN_POINT('Ctrl Pts',(-17.734,5.33320157527804,7.47778296865981));
#207810=CARTESIAN_POINT('Ctrl Pts',(-17.734,5.30659247765412,7.33623756953797));
#207811=CARTESIAN_POINT('Ctrl Pts',(-17.734,5.28636445802549,7.19365980491143));
#207812=CARTESIAN_POINT('Ctrl Pts',(-17.734,5.27260711226952,7.05048093602787));
#207813=CARTESIAN_POINT('Ctrl Pts',(-17.734,5.2685667290597,7.00843085543087));
#207814=CARTESIAN_POINT('Ctrl Pts',(-17.734,5.26508476885768,6.96632877290582));
#207815=CARTESIAN_POINT('Ctrl Pts',(-17.734,5.26216428318298,6.92418527139126));
#207816=CARTESIAN_POINT('Ctrl Pts',(-17.734,5.25225669184947,6.78121569821777));
#207817=CARTESIAN_POINT('Ctrl Pts',(-17.734,5.24880693790303,6.63777018725341));
#207818=CARTESIAN_POINT('Ctrl Pts',(-17.734,5.25169843615224,6.49425035729583));
#207819=CARTESIAN_POINT('Ctrl Pts',(-17.734,5.25418827323925,6.37066702279185));
#207820=CARTESIAN_POINT('Ctrl Pts',(-17.734,5.26138083595832,6.24702806280391));
#207821=CARTESIAN_POINT('Ctrl Pts',(-17.734,5.27323254549849,6.12358757186399));
#207822=CARTESIAN_POINT('Ctrl Pts',(-17.734,5.27508188116906,6.10432597063131));
#207823=CARTESIAN_POINT('Ctrl Pts',(-17.734,5.27704501035193,6.08506650230671));
#207824=CARTESIAN_POINT('Ctrl Pts',(-17.734,5.27912085414996,6.06581909013264));
#207825=CARTESIAN_POINT('Ctrl Pts',(-17.734,5.29479715330723,5.92046702099761));
#207826=CARTESIAN_POINT('Ctrl Pts',(-17.734,5.31686509682758,5.77608379440672));
#207827=CARTESIAN_POINT('Ctrl Pts',(-17.734,5.34513749586769,5.63308999580947));
#207828=CARTESIAN_POINT('Ctrl Pts',(-17.734,5.37370011526018,5.48862834474738));
#207829=CARTESIAN_POINT('Ctrl Pts',(-17.734,5.40859521040085,5.34558404093898));
#207830=CARTESIAN_POINT('Ctrl Pts',(-17.734,5.44968220909514,5.20437948161231));
#207831=CARTESIAN_POINT('Ctrl Pts',(-17.734,5.49084209463958,5.06292443050275));
#207832=CARTESIAN_POINT('Ctrl Pts',(-17.734,5.53821592674961,4.9233148595374));
#207833=CARTESIAN_POINT('Ctrl Pts',(-17.734,5.59171431210286,4.78597586977869));
#207834=CARTESIAN_POINT('Ctrl Pts',(-17.734,5.62179155274454,4.70876273863118));
#207835=CARTESIAN_POINT('Ctrl Pts',(-17.734,5.65380556163705,4.63226736340509));
#207836=CARTESIAN_POINT('Ctrl Pts',(-17.734,5.68774754568469,4.55656680513933));
#207837=CARTESIAN_POINT('Ctrl Pts',(-17.734,5.73801817128877,4.44444859728045));
#207838=CARTESIAN_POINT('Ctrl Pts',(-17.734,5.7925169840286,4.3340732964859));
#207839=CARTESIAN_POINT('Ctrl Pts',(-17.734,5.85109760638757,4.22562345682714));
#207840=CARTESIAN_POINT('Ctrl Pts',(-23.534,5.20509380555676,8.32288496556915));
#207841=CARTESIAN_POINT('Ctrl Pts',(-23.534,5.25448034822735,8.46102114255294));
#207842=CARTESIAN_POINT('Ctrl Pts',(-23.534,5.30984160896073,8.59666377487398));
#207843=CARTESIAN_POINT('Ctrl Pts',(-23.534,5.37090550416418,8.72949042856166));
#207844=CARTESIAN_POINT('Ctrl Pts',(-23.534,5.43261983427359,8.86373191325075));
#207845=CARTESIAN_POINT('Ctrl Pts',(-23.534,5.50015936697075,8.99509777454297));
#207846=CARTESIAN_POINT('Ctrl Pts',(-23.534,5.57328932777325,9.12322955612724));
#207847=CARTESIAN_POINT('Ctrl Pts',(-23.534,5.64611803495858,9.25083350804698));
#207848=CARTESIAN_POINT('Ctrl Pts',(-23.534,5.72449172930617,9.37523055725192));
#207849=CARTESIAN_POINT('Ctrl Pts',(-23.534,5.80821663878109,9.49603209760072));
#207850=CARTESIAN_POINT('Ctrl Pts',(-23.534,5.89053472328053,9.61480381641726));
#207851=CARTESIAN_POINT('Ctrl Pts',(-23.534,5.97802623664759,9.73010029344401));
#207852=CARTESIAN_POINT('Ctrl Pts',(-23.534,6.07053600560125,9.84151116234556));
#207853=CARTESIAN_POINT('Ctrl Pts',(-23.534,6.09530240301151,9.8713376972753));
#207854=CARTESIAN_POINT('Ctrl Pts',(-23.534,6.1204286083341,9.90088549066091));
#207855=CARTESIAN_POINT('Ctrl Pts',(-23.534,6.14591193093455,9.93014609427624));
#207856=CARTESIAN_POINT('Ctrl Pts',(-23.534,6.15955451065975,9.94581085369119));
#207857=CARTESIAN_POINT('Ctrl Pts',(-23.534,6.1732994431912,9.9613932992639));
#207858=CARTESIAN_POINT('Ctrl Pts',(-23.534,6.18714632818517,9.97689210391278));
#207859=CARTESIAN_POINT('Ctrl Pts',(-23.534,6.19947043338816,9.99068646265098));
#207860=CARTESIAN_POINT('Ctrl Pts',(-23.534,6.21187374698249,10.0044127646295));
#207861=CARTESIAN_POINT('Ctrl Pts',(-23.534,6.2243484693293,10.0180621311511));
#207862=CARTESIAN_POINT('Ctrl Pts',(-23.534,6.32643586438779,10.1297622743404));
#207863=CARTESIAN_POINT('Ctrl Pts',(-23.534,6.43344023196213,10.2364692341204));
#207864=CARTESIAN_POINT('Ctrl Pts',(-23.534,6.54511720413425,10.3377902027729));
#207865=CARTESIAN_POINT('Ctrl Pts',(-23.5339999999999,6.65173379038045,
10.4345200440534));
#207866=CARTESIAN_POINT('Ctrl Pts',(-23.534,6.76261007331514,10.5263410649745));
#207867=CARTESIAN_POINT('Ctrl Pts',(-23.534,6.87736332873699,10.6130492088599));
#207868=CARTESIAN_POINT('Ctrl Pts',(-23.5339999999999,6.99147784435786,
10.6992747177004));
#207869=CARTESIAN_POINT('Ctrl Pts',(-23.5339999999999,7.10942705472184,
10.7804443794007));
#207870=CARTESIAN_POINT('Ctrl Pts',(-23.5339999999999,7.23085436779322,
10.8563105129933));
#207871=CARTESIAN_POINT('Ctrl Pts',(-23.5339999999999,7.33613170340885,
10.9220863603382));
#207872=CARTESIAN_POINT('Ctrl Pts',(-23.534,7.44402406928014,10.9838750073567));
#207873=CARTESIAN_POINT('Ctrl Pts',(-23.534,7.55430465571587,11.0414837770386));
#207874=CARTESIAN_POINT('Ctrl Pts',(-23.534,7.58853359014114,11.059364411006));
#207875=CARTESIAN_POINT('Ctrl Pts',(-23.5339999999999,7.62299261107083,
11.0768421517888));
#207876=CARTESIAN_POINT('Ctrl Pts',(-23.534,7.65767495108206,11.0939106313755));
#207877=CARTESIAN_POINT('Ctrl Pts',(-23.534,7.68146530654451,11.1056187570799));
#207878=CARTESIAN_POINT('Ctrl Pts',(-23.5339999999999,7.70536587584369,
11.1171366355578));
#207879=CARTESIAN_POINT('Ctrl Pts',(-23.5339999999999,7.72934494066839,
11.1284484864467));
#207880=CARTESIAN_POINT('Ctrl Pts',(-23.534,7.85661864731222,11.1884884088606));
#207881=CARTESIAN_POINT('Ctrl Pts',(-23.5339999999999,7.98623315832197,
11.2427954978079));
#207882=CARTESIAN_POINT('Ctrl Pts',(-23.534,8.11783022540222,11.2911803845138));
#207883=CARTESIAN_POINT('Ctrl Pts',(-23.534,8.2483999926991,11.3391875592788));
#207884=CARTESIAN_POINT('Ctrl Pts',(-23.534,8.38092221481638,11.3813648380392));
#207885=CARTESIAN_POINT('Ctrl Pts',(-23.534,8.51505911917084,11.4174776458748));
#207886=CARTESIAN_POINT('Ctrl Pts',(-23.534,8.54046938028188,11.4243186854901));
#207887=CARTESIAN_POINT('Ctrl Pts',(-23.534,8.56593760257076,11.430941947973));
#207888=CARTESIAN_POINT('Ctrl Pts',(-23.534,8.59146150656054,11.4373456266197));
#207889=CARTESIAN_POINT('Ctrl Pts',(-23.534,8.7269958712635,11.4713497710281));
#207890=CARTESIAN_POINT('Ctrl Pts',(-23.534,8.86410085374641,11.4991663722465));
#207891=CARTESIAN_POINT('Ctrl Pts',(-23.534,9.00234645392465,11.5207487445334));
#207892=CARTESIAN_POINT('Ctrl Pts',(-23.534,9.11948261257159,11.5390355918611));
#207893=CARTESIAN_POINT('Ctrl Pts',(-23.534,9.2374378836336,11.5528458391875));
#207894=CARTESIAN_POINT('Ctrl Pts',(-23.534,9.355943158363,11.5621227489501));
#207895=CARTESIAN_POINT('Ctrl Pts',(-23.534,9.38621145908859,11.5644922324617));
#207896=CARTESIAN_POINT('Ctrl Pts',(-23.5339999999999,9.41651558906432,
11.5665658392786));
#207897=CARTESIAN_POINT('Ctrl Pts',(-23.5339999999999,9.44685094557672,
11.5683423557483));
#207898=CARTESIAN_POINT('Ctrl Pts',(-23.5339999999999,9.46479541432074,
11.5693932299733));
#207899=CARTESIAN_POINT('Ctrl Pts',(-23.534,9.48274095025218,11.5703395658612));
#207900=CARTESIAN_POINT('Ctrl Pts',(-23.534,9.50068594451741,11.5711814160656));
#207901=CARTESIAN_POINT('Ctrl Pts',(-23.534,9.6376789645452,11.5776081443338));
#207902=CARTESIAN_POINT('Ctrl Pts',(-23.534,9.77465402965032,11.5779506548684));
#207903=CARTESIAN_POINT('Ctrl Pts',(-23.534,9.91120575942693,11.572220826072));
#207904=CARTESIAN_POINT('Ctrl Pts',(-23.534,10.0465379651817,11.5665421695593));
#207905=CARTESIAN_POINT('Ctrl Pts',(-23.534,10.1814551280495,11.5548989762848));
#207906=CARTESIAN_POINT('Ctrl Pts',(-23.5339999999999,10.3155540558513,
11.5372529906715));
#207907=CARTESIAN_POINT('Ctrl Pts',(-23.5339999999999,10.4488851811288,
11.5197080396639));
#207908=CARTESIAN_POINT('Ctrl Pts',(-23.534,10.5814081302335,11.4962287057346));
#207909=CARTESIAN_POINT('Ctrl Pts',(-23.5339999999999,10.7127070778146,
11.466730168397));
#207910=CARTESIAN_POINT('Ctrl Pts',(-23.5339999999999,10.7477535156779,
11.4588563912274));
#207911=CARTESIAN_POINT('Ctrl Pts',(-23.534,10.7827126062386,11.4505535095437));
#207912=CARTESIAN_POINT('Ctrl Pts',(-23.534,10.8175761048042,11.4418193551064));
#207913=CARTESIAN_POINT('Ctrl Pts',(-23.534,10.9043442667858,11.4200818199142));
#207914=CARTESIAN_POINT('Ctrl Pts',(-23.534,10.9905208003715,11.3956733994087));
#207915=CARTESIAN_POINT('Ctrl Pts',(-23.534,11.0759855672366,11.3686310737129));
#207916=CARTESIAN_POINT('Ctrl Pts',(-23.534,11.1080452454195,11.3584869138336));
#207917=CARTESIAN_POINT('Ctrl Pts',(-23.5339999999999,11.1400046970052,
11.3479720510328));
#207918=CARTESIAN_POINT('Ctrl Pts',(-23.534,11.1718573159444,11.3370881949364));
#207919=CARTESIAN_POINT('Ctrl Pts',(-23.534,11.1899003611931,11.3309229904864));
#207920=CARTESIAN_POINT('Ctrl Pts',(-23.5339999999999,11.2079056979589,
11.3246405183814));
#207921=CARTESIAN_POINT('Ctrl Pts',(-23.5339999999999,11.2258644852499,
11.3182440453307));
#207922=CARTESIAN_POINT('Ctrl Pts',(-23.5339999999999,11.3524381725536,
11.2731616482488));
#207923=CARTESIAN_POINT('Ctrl Pts',(-23.534,11.4768170268763,11.2223807678744));
#207924=CARTESIAN_POINT('Ctrl Pts',(-23.534,11.5986229667085,11.1660898819114));
#207925=CARTESIAN_POINT('Ctrl Pts',(-23.534,11.7193673208799,11.1102895926916));
#207926=CARTESIAN_POINT('Ctrl Pts',(-23.534,11.8375840317477,11.0490744065508));
#207927=CARTESIAN_POINT('Ctrl Pts',(-23.534,11.9528722695249,10.9825889536062));
#207928=CARTESIAN_POINT('Ctrl Pts',(-23.534,12.0079182811876,10.9508445268654));
#207929=CARTESIAN_POINT('Ctrl Pts',(-23.534,12.0622961454576,10.9178981000385));
#207930=CARTESIAN_POINT('Ctrl Pts',(-23.534,12.115958959572,10.8837627538526));
#207931=CARTESIAN_POINT('Ctrl Pts',(-23.534,12.1331643569177,10.8728182626933));
#207932=CARTESIAN_POINT('Ctrl Pts',(-23.534,12.150294211089,10.8617527782972));
#207933=CARTESIAN_POINT('Ctrl Pts',(-23.534,12.1673397958196,10.8505716388401));
#207934=CARTESIAN_POINT('Ctrl Pts',(-23.5339999999999,12.2766355142431,
10.7788785471058));
#207935=CARTESIAN_POINT('Ctrl Pts',(-23.534,12.3825568873876,10.7023781389818));
#207936=CARTESIAN_POINT('Ctrl Pts',(-23.534,12.4847306195173,10.6212230158632));
#207937=CARTESIAN_POINT('Ctrl Pts',(-23.534,12.5574317395047,10.5634775638721));
#207938=CARTESIAN_POINT('Ctrl Pts',(-23.534,12.6282347834106,10.503374641833));
#207939=CARTESIAN_POINT('Ctrl Pts',(-23.534,12.6969925515033,10.4409593113222));
#207940=CARTESIAN_POINT('Ctrl Pts',(-23.534,12.7737176242397,10.3713116059626));
#207941=CARTESIAN_POINT('Ctrl Pts',(-23.534,12.8478962945781,10.2987843938166));
#207942=CARTESIAN_POINT('Ctrl Pts',(-23.5339999999999,12.9193848394627,
10.2235362295063));
#207943=CARTESIAN_POINT('Ctrl Pts',(23.5309283172883,7.34300535603735,3.78082119416608));
#207944=CARTESIAN_POINT('Ctrl Pts',(23.4921425539738,7.86601024404076,3.32811163657506));
#207945=CARTESIAN_POINT('Ctrl Pts',(23.4145749090232,9.13626656589345,2.68283027075003));
#207946=CARTESIAN_POINT('Ctrl Pts',(23.2982253824366,11.2738498134804,2.72043220540736));
#207947=CARTESIAN_POINT('Ctrl Pts',(23.1818797375284,13.1445654280131,3.75450519529614));
#207948=CARTESIAN_POINT('Ctrl Pts',(23.0655340926202,14.3134104771639,5.54427759941156));
#207949=CARTESIAN_POINT('Ctrl Pts',(22.949188447712,14.5079780693299,7.67300394796904));
#207950=CARTESIAN_POINT('Ctrl Pts',(22.8328428028038,13.6830822571742,9.64502652688917));
#207951=CARTESIAN_POINT('Ctrl Pts',(22.7164971578956,12.0307386115573,11.0011705393577));
#207952=CARTESIAN_POINT('Ctrl Pts',(22.6001515129874,9.93571184213651,11.4256669327143));
#207953=CARTESIAN_POINT('Ctrl Pts',(22.4838058680792,7.88580366311466,10.8196740498626));
#207954=CARTESIAN_POINT('Ctrl Pts',(22.367460223171,6.35832750127234,9.32429364407502));
#207955=CARTESIAN_POINT('Ctrl Pts',(22.2511145782628,5.70894628402538,7.28771595678545));
#207956=CARTESIAN_POINT('Ctrl Pts',(22.1347689333546,6.08886062127945,5.18414506891689));
#207957=CARTESIAN_POINT('Ctrl Pts',(22.0184232884464,7.40962001767397,3.50338546661371));
#207958=CARTESIAN_POINT('Ctrl Pts',(21.9020776435382,9.36367135867349,2.63678951113586));
#207959=CARTESIAN_POINT('Ctrl Pts',(21.78573199863,11.4960733546058,2.78614318046246));
#207960=CARTESIAN_POINT('Ctrl Pts',(21.6693863537218,13.3102097615393,3.91666104806278));
#207961=CARTESIAN_POINT('Ctrl Pts',(21.5530407088136,14.3838786712727,5.76512857483606));
#207962=CARTESIAN_POINT('Ctrl Pts',(21.4366950639055,14.4666465134933,7.90110058902803));
#207963=CARTESIAN_POINT('Ctrl Pts',(21.3203494189972,13.5401544226926,9.82731484321649));
#207964=CARTESIAN_POINT('Ctrl Pts',(21.2040037740891,11.818219849542,11.0950850634552));
#207965=CARTESIAN_POINT('Ctrl Pts',(21.0876581291808,9.70578223018301,11.4095937069531));
#207966=CARTESIAN_POINT('Ctrl Pts',(20.9713124842727,7.68634952883146,10.6968241722325));
#207967=CARTESIAN_POINT('Ctrl Pts',(20.8549668393645,6.24762631375591,9.12439123907643));
#207968=CARTESIAN_POINT('Ctrl Pts',(20.6998393128202,5.50252433774221,6.36487623709474));
#207969=CARTESIAN_POINT('Ctrl Pts',(20.5059299046399,7.26489001546572,2.90530097391561));
#207970=CARTESIAN_POINT('Ctrl Pts',(20.2732386148235,11.9254850147715,2.33663337229139));
#207971=CARTESIAN_POINT('Ctrl Pts',(20.0793292066432,14.4680075562826,5.27094298607233));
#207972=CARTESIAN_POINT('Ctrl Pts',(19.9242016800989,14.4082980438857,8.12865794298295));
#207973=CARTESIAN_POINT('Ctrl Pts',(19.8078560351907,13.3898808093813,10.0009015583641));
#207974=CARTESIAN_POINT('Ctrl Pts',(19.6915103902825,11.6010834707722,11.1783364509586));
#207975=CARTESIAN_POINT('Ctrl Pts',(19.5751647453743,9.47499843604004,11.3809957897657));
#207976=CARTESIAN_POINT('Ctrl Pts',(19.4588191004661,7.49874546760186,10.5644639714789));
#207977=CARTESIAN_POINT('Ctrl Pts',(19.3424734555579,6.1362730321213,8.91754023010204));
#207978=CARTESIAN_POINT('Ctrl Pts',(19.2261278106497,5.70301304802592,6.82433389834715));
#207979=CARTESIAN_POINT('Ctrl Pts',(19.1097821657415,6.3007131588549,4.77193245058443));
#207980=CARTESIAN_POINT('Ctrl Pts',(18.9934365208334,7.78978883331376,3.23836954425806));
#207981=CARTESIAN_POINT('Ctrl Pts',(18.8770908759252,9.82371572424119,2.58065669417856));
#207982=CARTESIAN_POINT('Ctrl Pts',(18.760745231017,11.9288120776716,2.95197129944819));
#207983=CARTESIAN_POINT('Ctrl Pts',(18.6443995861088,13.6149642392687,4.26583929580108));
#207984=CARTESIAN_POINT('Ctrl Pts',(18.5280539412006,14.4895408169203,6.21634210117263));
#207985=CARTESIAN_POINT('Ctrl Pts',(18.4117082962924,14.3489117283966,8.34931376088588));
#207986=CARTESIAN_POINT('Ctrl Pts',(18.2953626513842,13.225818013417,10.1681063522451));
#207987=CARTESIAN_POINT('Ctrl Pts',(18.179017006476,11.3817646217731,11.2492252195552));
#207988=CARTESIAN_POINT('Ctrl Pts',(18.0626713615678,9.24613280585004,11.3409372655453));
#207989=CARTESIAN_POINT('Ctrl Pts',(17.9463257166596,7.31617934650269,10.421891156518));
#207990=CARTESIAN_POINT('Ctrl Pts',(17.8299800717514,6.04130773120048,8.70607399924876));
#207991=CARTESIAN_POINT('Ctrl Pts',(17.7136344268432,5.71830963515471,6.59301823923793));
#207992=CARTESIAN_POINT('Ctrl Pts',(17.597288781935,6.42250688754369,4.57470452794694));
#207993=CARTESIAN_POINT('Ctrl Pts',(17.4809431370268,7.9896921867418,3.1211522939865));
#207994=CARTESIAN_POINT('Ctrl Pts',(17.3645974921186,10.0554503632162,2.57068500932872));
#207995=CARTESIAN_POINT('Ctrl Pts',(17.2870337288465,11.4435279727104,2.89154782505743));
#207996=CARTESIAN_POINT('Ctrl Pts',(17.2482518472104,12.0599972964235,3.20515550067288));
#207997=CARTESIAN_POINT('Ctrl Pts',(23.6935169503155,7.15869994272444,3.56789701660741));
#207998=CARTESIAN_POINT('Ctrl Pts',(23.654731187001,7.71629762359647,3.08524416725256));
#207999=CARTESIAN_POINT('Ctrl Pts',(23.5771635420504,9.07057173350399,2.39728235016981));
#208000=CARTESIAN_POINT('Ctrl Pts',(23.4608140154638,11.3495398442526,2.43737136662486));
#208001=CARTESIAN_POINT('Ctrl Pts',(23.3444683705557,13.3439890590901,3.53984041469738));
#208002=CARTESIAN_POINT('Ctrl Pts',(23.2281227256474,14.5901443124249,5.44799264178905));
#208003=CARTESIAN_POINT('Ctrl Pts',(23.1117770807393,14.7975810700024,7.71751803704522));
#208004=CARTESIAN_POINT('Ctrl Pts',(22.9954314358311,13.9181246779694,9.81997490093976));
#208005=CARTESIAN_POINT('Ctrl Pts',(22.8790857909229,12.1564910758115,11.2658175185254));
#208006=CARTESIAN_POINT('Ctrl Pts',(22.7627401460147,9.92289423037199,11.7183911175558));
#208007=CARTESIAN_POINT('Ctrl Pts',(22.6463945011065,7.73740022669883,11.0723164175793));
#208008=CARTESIAN_POINT('Ctrl Pts',(22.5300488561983,6.10889314202882,9.47802797895342));
#208009=CARTESIAN_POINT('Ctrl Pts',(22.4137032112901,5.41656029955566,7.30674617758523));
#208010=CARTESIAN_POINT('Ctrl Pts',(22.2973575663819,5.82160307877634,5.06404008528999));
#208011=CARTESIAN_POINT('Ctrl Pts',(22.1810119214737,7.22972065723908,3.2721110271785));
#208012=CARTESIAN_POINT('Ctrl Pts',(22.0646662765655,9.3130176225996,2.34819634471306));
#208013=CARTESIAN_POINT('Ctrl Pts',(21.9483206316573,11.5864617813299,2.50742862256836));
#208014=CARTESIAN_POINT('Ctrl Pts',(21.8319749867491,13.5205895045972,3.71272164299274));
#208015=CARTESIAN_POINT('Ctrl Pts',(21.7156293418409,14.6652734412564,5.68345122839067));
#208016=CARTESIAN_POINT('Ctrl Pts',(21.5992836969327,14.7535157463124,7.96070153491793));
#208017=CARTESIAN_POINT('Ctrl Pts',(21.4829380520245,13.7657432550285,10.0143202020366));
#208018=CARTESIAN_POINT('Ctrl Pts',(21.3665924071164,11.9299158151215,11.3659437736297));
#208019=CARTESIAN_POINT('Ctrl Pts',(21.2502467622081,9.67775652453044,11.7012547702403));
#208020=CARTESIAN_POINT('Ctrl Pts',(21.1339011172999,7.52475371943345,10.9413409555267));
#208021=CARTESIAN_POINT('Ctrl Pts',(21.0175554723918,5.99086991348007,9.26490355127649));
#208022=CARTESIAN_POINT('Ctrl Pts',(20.8624279458475,5.19648511255694,6.32286763396294));
#208023=CARTESIAN_POINT('Ctrl Pts',(20.6685185376672,7.07541786689233,2.63446779717522));
#208024=CARTESIAN_POINT('Ctrl Pts',(20.4358272478508,12.0442757546598,2.02818716170503));
#208025=CARTESIAN_POINT('Ctrl Pts',(20.2419178396704,14.7549668117235,5.1565790240658));
#208026=CARTESIAN_POINT('Ctrl Pts',(20.0867903131262,14.6913079695174,8.20331007594904));
#208027=CARTESIAN_POINT('Ctrl Pts',(19.970444668218,13.6055301858954,10.1993883572618));
#208028=CARTESIAN_POINT('Ctrl Pts',(19.8540990233098,11.6984175174723,11.4547016068087));
#208029=CARTESIAN_POINT('Ctrl Pts',(19.7377533784016,9.43170813884858,11.6707653184832));
#208030=CARTESIAN_POINT('Ctrl Pts',(19.6214077334934,7.32474107736591,10.8002261348571));
#208031=CARTESIAN_POINT('Ctrl Pts',(19.5050620885852,5.87215145975016,9.04437092235506));
#208032=CARTESIAN_POINT('Ctrl Pts',(19.388716443677,5.41023462515135,6.81271492267807));
#208033=CARTESIAN_POINT('Ctrl Pts',(19.2723707987688,6.04746804935031,4.62456273951254));
#208034=CARTESIAN_POINT('Ctrl Pts',(19.1560251538606,7.63503474665393,2.98956631853571));
#208035=CARTESIAN_POINT('Ctrl Pts',(19.0396795089524,9.80349042165522,2.28835076912831));
#208036=CARTESIAN_POINT('Ctrl Pts',(18.9233338640442,12.0478228774492,2.68422500954442));
#208037=CARTESIAN_POINT('Ctrl Pts',(18.806988219136,13.8455011716103,4.08499537430166));
#208038=CARTESIAN_POINT('Ctrl Pts',(18.6906425742278,14.7779243336677,6.16450909540956));
#208039=CARTESIAN_POINT('Ctrl Pts',(18.5742969293197,14.6279937012347,8.43856059684434));
#208040=CARTESIAN_POINT('Ctrl Pts',(18.4579512844115,13.4306158846232,10.3776524756999));
#208041=CARTESIAN_POINT('Ctrl Pts',(18.3416056395033,11.4645923957984,11.5302791279295));
#208042=CARTESIAN_POINT('Ctrl Pts',(18.2252599945951,9.18770478906643,11.628057227762));
#208043=CARTESIAN_POINT('Ctrl Pts',(18.1089143496868,7.13009959682579,10.6482232132763));
#208044=CARTESIAN_POINT('Ctrl Pts',(17.9925687047787,5.77090492693302,8.81891780975284));
#208045=CARTESIAN_POINT('Ctrl Pts',(17.8762230598705,5.42654296509983,6.56609949321034));
#208046=CARTESIAN_POINT('Ctrl Pts',(17.7598774149623,6.17731750624712,4.41428969085003));
#208047=CARTESIAN_POINT('Ctrl Pts',(17.6435317700541,7.84816018549169,2.86459603927288));
#208048=CARTESIAN_POINT('Ctrl Pts',(17.5271861251459,10.0505525433181,2.27771953321792));
#208049=CARTESIAN_POINT('Ctrl Pts',(17.4496223618738,11.5304409223333,2.61980498219221));
#208050=CARTESIAN_POINT('Ctrl Pts',(17.4108404802377,12.1876850000003,2.954155418752));
#208051=CARTESIAN_POINT('Ctrl Pts',(23.8561055833427,6.97439452941152,3.35497283904874));
#208052=CARTESIAN_POINT('Ctrl Pts',(23.8173198200282,7.56658500315218,2.84237669793006));
#208053=CARTESIAN_POINT('Ctrl Pts',(23.7397521750777,9.00487690111454,2.11173442958961));
#208054=CARTESIAN_POINT('Ctrl Pts',(23.6234026484911,11.4252298750248,2.15431052784236));
#208055=CARTESIAN_POINT('Ctrl Pts',(23.5070570035829,13.543412690167,3.32517563409861));
#208056=CARTESIAN_POINT('Ctrl Pts',(23.3907113586747,14.8668781476858,5.35170768416653));
#208057=CARTESIAN_POINT('Ctrl Pts',(23.2743657137665,15.0871840706748,7.7620321261214));
#208058=CARTESIAN_POINT('Ctrl Pts',(23.1580200688583,14.1531670987647,9.99492327499034));
#208059=CARTESIAN_POINT('Ctrl Pts',(23.0416744239502,12.2822435400657,11.5304644976931));
#208060=CARTESIAN_POINT('Ctrl Pts',(22.925328779042,9.91007661860751,12.0111153023973));
#208061=CARTESIAN_POINT('Ctrl Pts',(22.8089831341337,7.58899679028301,11.324958785296));
#208062=CARTESIAN_POINT('Ctrl Pts',(22.6926374892256,5.85945878278532,9.63176231383182));
#208063=CARTESIAN_POINT('Ctrl Pts',(22.5762918443174,5.12417431508593,7.32577639838504));
#208064=CARTESIAN_POINT('Ctrl Pts',(22.4599461994092,5.55434553627324,4.94393510166309));
#208065=CARTESIAN_POINT('Ctrl Pts',(22.343600554501,7.04982129680419,3.04083658774328));
#208066=CARTESIAN_POINT('Ctrl Pts',(22.2272549095928,9.26236388652573,2.05960317829026));
#208067=CARTESIAN_POINT('Ctrl Pts',(22.1109092646846,11.6768502080541,2.22871406467427));
#208068=CARTESIAN_POINT('Ctrl Pts',(21.9945636197764,13.730969247655,3.50878223792271));
#208069=CARTESIAN_POINT('Ctrl Pts',(21.8782179748682,14.9466682112401,5.60177388194529));
#208070=CARTESIAN_POINT('Ctrl Pts',(21.76187232996,15.0403849791315,8.02030248080784));
#208071=CARTESIAN_POINT('Ctrl Pts',(21.6455266850518,13.9913320873644,10.2013255608568));
#208072=CARTESIAN_POINT('Ctrl Pts',(21.5291810401436,12.041611780701,11.6368024838041));
#208073=CARTESIAN_POINT('Ctrl Pts',(21.4128353952354,9.64973081887787,11.9929158335273));
#208074=CARTESIAN_POINT('Ctrl Pts',(21.2964897503273,7.36315791003544,11.185857738821));
#208075=CARTESIAN_POINT('Ctrl Pts',(21.180144105419,5.73411351320423,9.40541586347656));
#208076=CARTESIAN_POINT('Ctrl Pts',(21.0250165788748,4.89044588737168,6.28085903083115));
#208077=CARTESIAN_POINT('Ctrl Pts',(20.8311071706945,6.88594571831891,2.36363462043484));
#208078=CARTESIAN_POINT('Ctrl Pts',(20.598415880878,12.1630664945482,1.71974095111867));
#208079=CARTESIAN_POINT('Ctrl Pts',(20.4045064726977,15.0419260671645,5.04221506205927));
#208080=CARTESIAN_POINT('Ctrl Pts',(20.2493789461535,14.9743178951491,8.27796220891513));
#208081=CARTESIAN_POINT('Ctrl Pts',(20.1330333012453,13.8211795624095,10.3978751561594));
#208082=CARTESIAN_POINT('Ctrl Pts',(20.0166876563371,11.7957515641725,11.7310667626589));
#208083=CARTESIAN_POINT('Ctrl Pts',(19.9003420114289,9.3884178416571,11.9605348472007));
#208084=CARTESIAN_POINT('Ctrl Pts',(19.7839963665207,7.15073668712996,11.0359882982353));
#208085=CARTESIAN_POINT('Ctrl Pts',(19.6676507216125,5.60802988737902,9.17120161460807));
#208086=CARTESIAN_POINT('Ctrl Pts',(19.5513050767043,5.11745620227678,6.80109594700901));
#208087=CARTESIAN_POINT('Ctrl Pts',(19.4349594317961,5.79422293984571,4.47719302844065));
#208088=CARTESIAN_POINT('Ctrl Pts',(19.3186137868879,7.4802806599941,2.74076309281336));
#208089=CARTESIAN_POINT('Ctrl Pts',(19.2022681419797,9.78326511906926,1.99604484407805));
#208090=CARTESIAN_POINT('Ctrl Pts',(19.0859224970715,12.1668336772269,2.41647871964064));
#208091=CARTESIAN_POINT('Ctrl Pts',(18.9695768521633,14.0760381039521,3.90415145280225));
#208092=CARTESIAN_POINT('Ctrl Pts',(18.8532312072551,15.0663078504151,6.11267608964647));
#208093=CARTESIAN_POINT('Ctrl Pts',(18.7368855623469,14.9070756740727,8.52780743280282));
#208094=CARTESIAN_POINT('Ctrl Pts',(18.6205399174387,13.6354137558295,10.5871985991546));
#208095=CARTESIAN_POINT('Ctrl Pts',(18.5041942725306,11.5474201698238,11.8113330363039));
#208096=CARTESIAN_POINT('Ctrl Pts',(18.3878486276223,9.12927677228282,11.9151771899788));
#208097=CARTESIAN_POINT('Ctrl Pts',(18.2715029827142,6.94401984714889,10.8745552700345));
#208098=CARTESIAN_POINT('Ctrl Pts',(18.155157337806,5.50050212266556,8.93176162025691));
#208099=CARTESIAN_POINT('Ctrl Pts',(18.0388116928978,5.13477629504494,6.53918074718275));
#208100=CARTESIAN_POINT('Ctrl Pts',(17.9224660479896,5.93212812495056,4.25387485375313));
#208101=CARTESIAN_POINT('Ctrl Pts',(17.8061204030814,7.70662818424157,2.60803978455923));
#208102=CARTESIAN_POINT('Ctrl Pts',(17.6897747581732,10.0456547234199,1.9847540571071));
#208103=CARTESIAN_POINT('Ctrl Pts',(17.612210994901,11.6173538719561,2.34806213932699));
#208104=CARTESIAN_POINT('Ctrl Pts',(17.573429113265,12.3153727035772,2.70315533683113));
#208105=CARTESIAN_POINT('Ctrl Pts',(24.01869421637,6.79008911609861,3.14204866149007));
#208106=CARTESIAN_POINT('Ctrl Pts',(23.9799084530555,7.4168723827079,2.59950922860756));
#208107=CARTESIAN_POINT('Ctrl Pts',(23.902340808105,8.93918206872512,1.8261865090094));
#208108=CARTESIAN_POINT('Ctrl Pts',(23.7859912815184,11.500919905797,1.87124968905985));
#208109=CARTESIAN_POINT('Ctrl Pts',(23.6696456366102,13.7428363212439,3.11051085349985));
#208110=CARTESIAN_POINT('Ctrl Pts',(23.553299991702,15.1436119829468,5.25542272654401));
#208111=CARTESIAN_POINT('Ctrl Pts',(23.4369543467938,15.3767870713474,7.80654621519758));
#208112=CARTESIAN_POINT('Ctrl Pts',(23.3206087018856,14.3882095195599,10.169871649041));
#208113=CARTESIAN_POINT('Ctrl Pts',(23.2042630569774,12.40799600432,11.7951114768609));
#208114=CARTESIAN_POINT('Ctrl Pts',(23.0879174120693,9.89725900684299,12.3038394872388));
#208115=CARTESIAN_POINT('Ctrl Pts',(22.971571767161,7.4405933538672,11.5776011530127));
#208116=CARTESIAN_POINT('Ctrl Pts',(22.8552261222528,5.6100244235418,9.78549664871022));
#208117=CARTESIAN_POINT('Ctrl Pts',(22.7388804773446,4.83178833061622,7.34480661918484));
#208118=CARTESIAN_POINT('Ctrl Pts',(22.6225348324365,5.28708799377012,4.82383011803619));
#208119=CARTESIAN_POINT('Ctrl Pts',(22.5061891875283,6.86992193636931,2.80956214830806));
#208120=CARTESIAN_POINT('Ctrl Pts',(22.38984354262,9.21171015045184,1.77101001186746));
#208121=CARTESIAN_POINT('Ctrl Pts',(22.2734978977119,11.7672386347782,1.94999950678018));
#208122=CARTESIAN_POINT('Ctrl Pts',(22.1571522528037,13.9413489907128,3.30484283285267));
#208123=CARTESIAN_POINT('Ctrl Pts',(22.0408066078955,15.2280629812237,5.52009653549991));
#208124=CARTESIAN_POINT('Ctrl Pts',(21.9244609629873,15.3272542119506,8.07990342669773));
#208125=CARTESIAN_POINT('Ctrl Pts',(21.8081153180791,14.2169209197003,10.3883309196771));
#208126=CARTESIAN_POINT('Ctrl Pts',(21.6917696731709,12.1533077462805,11.9076611939785));
#208127=CARTESIAN_POINT('Ctrl Pts',(21.5754240282627,9.62170511322531,12.2845768968145));
#208128=CARTESIAN_POINT('Ctrl Pts',(21.4590783833545,7.20156210063743,11.4303745221154));
#208129=CARTESIAN_POINT('Ctrl Pts',(21.3427327384463,5.4773571129284,9.54592817567664));
#208130=CARTESIAN_POINT('Ctrl Pts',(21.187605211902,4.58440666218642,6.23885042769937));
#208131=CARTESIAN_POINT('Ctrl Pts',(20.9936958037217,6.69647356974549,2.09280144369445));
#208132=CARTESIAN_POINT('Ctrl Pts',(20.7610045139053,12.2818572344366,1.41129474053231));
#208133=CARTESIAN_POINT('Ctrl Pts',(20.567095105725,15.3288853226055,4.92785110005275));
#208134=CARTESIAN_POINT('Ctrl Pts',(20.4119675791808,15.2573278207807,8.3526143418812));
#208135=CARTESIAN_POINT('Ctrl Pts',(20.2956219342725,14.0368289389236,10.5963619550571));
#208136=CARTESIAN_POINT('Ctrl Pts',(20.1792762893644,11.8930856108726,12.007431918509));
#208137=CARTESIAN_POINT('Ctrl Pts',(20.0629306444561,9.34512754446563,12.2503043759182));
#208138=CARTESIAN_POINT('Ctrl Pts',(19.946584999548,6.97673229689402,11.2717504616136));
#208139=CARTESIAN_POINT('Ctrl Pts',(19.8302393546397,5.34390831500789,9.29803230686109));
#208140=CARTESIAN_POINT('Ctrl Pts',(19.7138937097316,4.82467777940222,6.78947697133994));
#208141=CARTESIAN_POINT('Ctrl Pts',(19.5975480648234,5.54097783034111,4.32982331736877));
#208142=CARTESIAN_POINT('Ctrl Pts',(19.4812024199152,7.32552657333427,2.49195986709101));
#208143=CARTESIAN_POINT('Ctrl Pts',(19.364856775007,9.7630398164833,1.7037389190278));
#208144=CARTESIAN_POINT('Ctrl Pts',(19.2485111300988,12.2858444770046,2.14873242973686));
#208145=CARTESIAN_POINT('Ctrl Pts',(19.1321654851906,14.3065750362938,3.72330753130284));
#208146=CARTESIAN_POINT('Ctrl Pts',(19.0158198402824,15.3546913671625,6.06084308388339));
#208147=CARTESIAN_POINT('Ctrl Pts',(18.8994741953742,15.1861576469106,8.61705426876128));
#208148=CARTESIAN_POINT('Ctrl Pts',(18.783128550466,13.8402116270357,10.7967447226094));
#208149=CARTESIAN_POINT('Ctrl Pts',(18.6667829055578,11.6302479438492,12.0923869446781));
#208150=CARTESIAN_POINT('Ctrl Pts',(18.5504372606496,9.07084875549921,12.2022971521955));
#208151=CARTESIAN_POINT('Ctrl Pts',(18.4340916157414,6.75794009747201,11.1008873267927));
#208152=CARTESIAN_POINT('Ctrl Pts',(18.3177459708332,5.23009931839809,9.04460543076101));
#208153=CARTESIAN_POINT('Ctrl Pts',(18.201400325925,4.84300962499006,6.51226200115517));
#208154=CARTESIAN_POINT('Ctrl Pts',(18.0850546810169,5.686938743654,4.09346001665621));
#208155=CARTESIAN_POINT('Ctrl Pts',(17.9687090361086,7.56509618299146,2.3514835298456));
#208156=CARTESIAN_POINT('Ctrl Pts',(17.8523633912005,10.0407569035218,1.69178858099628));
#208157=CARTESIAN_POINT('Ctrl Pts',(17.7747996279283,11.7042668215791,2.07631929646177));
#208158=CARTESIAN_POINT('Ctrl Pts',(17.7360177462923,12.4430604071541,2.45215525491025));
#208159=CARTESIAN_POINT('Ctrl Pts',(17.734,12.4414757859805,2.45527019889633));
#208160=CARTESIAN_POINT('Ctrl Pts',(17.734,12.3039867051776,2.39880617496762));
#208161=CARTESIAN_POINT('Ctrl Pts',(17.734,12.1641669931159,2.34855999836893));
#208162=CARTESIAN_POINT('Ctrl Pts',(17.734,12.0224504771058,2.30458254792744));
#208163=CARTESIAN_POINT('Ctrl Pts',(17.734,11.8806702981265,2.26058534160181));
#208164=CARTESIAN_POINT('Ctrl Pts',(17.734,11.7369908076955,2.22286244819522));
#208165=CARTESIAN_POINT('Ctrl Pts',(17.734,11.5918412571295,2.19151632686583));
#208166=CARTESIAN_POINT('Ctrl Pts',(17.734,11.5283759214344,2.17781051720157));
#208167=CARTESIAN_POINT('Ctrl Pts',(17.734,11.4646295455477,2.16532448469426));
#208168=CARTESIAN_POINT('Ctrl Pts',(17.734,11.4006382986832,2.15406992347917));
#208169=CARTESIAN_POINT('Ctrl Pts',(17.734,11.3633072808146,2.14750427198133));
#208170=CARTESIAN_POINT('Ctrl Pts',(17.734,11.3258921197711,2.14135763815236));
#208171=CARTESIAN_POINT('Ctrl Pts',(17.734,11.2884026214455,2.13563303349492));
#208172=CARTESIAN_POINT('Ctrl Pts',(17.734,11.2692561047233,2.13270938170716));
#208173=CARTESIAN_POINT('Ctrl Pts',(17.734,11.250091584631,2.12989604625388));
#208174=CARTESIAN_POINT('Ctrl Pts',(17.734,11.2309171197761,2.12719424914615));
#208175=CARTESIAN_POINT('Ctrl Pts',(17.734,11.0859964654593,2.10677405970945));
#208176=CARTESIAN_POINT('Ctrl Pts',(17.734,10.9403799749511,2.09270150463882));
#208177=CARTESIAN_POINT('Ctrl Pts',(17.734,10.7944837770183,2.0850637244268));
#208178=CARTESIAN_POINT('Ctrl Pts',(17.734,10.6507966464814,2.07754159062287));
#208179=CARTESIAN_POINT('Ctrl Pts',(17.734,10.5068375056611,2.07626094200617));
#208180=CARTESIAN_POINT('Ctrl Pts',(17.734,10.3630121887448,2.08135439022792));
#208181=CARTESIAN_POINT('Ctrl Pts',(17.734,10.2786127987142,2.08434332105237));
#208182=CARTESIAN_POINT('Ctrl Pts',(17.734,10.1942597021903,2.08952813543894));
#208183=CARTESIAN_POINT('Ctrl Pts',(17.734,10.1100377343263,2.0969435515888));
#208184=CARTESIAN_POINT('Ctrl Pts',(17.734,10.0914524803675,2.09857991079354));
#208185=CARTESIAN_POINT('Ctrl Pts',(17.734,10.0728758846397,2.10032474830959));
#208186=CARTESIAN_POINT('Ctrl Pts',(17.734,10.054317787698,2.10217740077462));
#208187=CARTESIAN_POINT('Ctrl Pts',(17.734,10.0520311372889,2.10240567679508));
#208188=CARTESIAN_POINT('Ctrl Pts',(17.734,10.0497447287136,2.1026355930538));
#208189=CARTESIAN_POINT('Ctrl Pts',(17.734,10.0474585635589,2.10286714977861));
#208190=CARTESIAN_POINT('Ctrl Pts',(17.734,9.90553857679408,2.11724167003299));
#208191=CARTESIAN_POINT('Ctrl Pts',(17.734,9.76455596495627,2.13793360360503));
#208192=CARTESIAN_POINT('Ctrl Pts',(17.734,9.62489441371198,2.164760150274));
#208193=CARTESIAN_POINT('Ctrl Pts',(17.734,9.4842370437923,2.19177797633183));
#208194=CARTESIAN_POINT('Ctrl Pts',(17.734,9.34491888101862,2.2250185138914));
#208195=CARTESIAN_POINT('Ctrl Pts',(17.734,9.2073470145511,2.26434539672021));
#208196=CARTESIAN_POINT('Ctrl Pts',(17.734,9.0710255779474,2.30331482631383));
#208197=CARTESIAN_POINT('Ctrl Pts',(17.734,8.93641816408468,2.34826086911714));
#208198=CARTESIAN_POINT('Ctrl Pts',(17.734,8.8039462971496,2.39909462227723));
#208199=CARTESIAN_POINT('Ctrl Pts',(17.734,8.67331233993274,2.44922310985069));
#208200=CARTESIAN_POINT('Ctrl Pts',(17.734,8.54475450125128,2.50507746381745));
#208201=CARTESIAN_POINT('Ctrl Pts',(17.734,8.4187110735798,2.56660924088476));
#208202=CARTESIAN_POINT('Ctrl Pts',(17.734,8.39060081781657,2.58033208247104));
#208203=CARTESIAN_POINT('Ctrl Pts',(17.734,8.36261638829719,2.59433712698117));
#208204=CARTESIAN_POINT('Ctrl Pts',(17.734,8.33476077291323,2.60862517471304));
#208205=CARTESIAN_POINT('Ctrl Pts',(17.734,8.31199475765094,2.62030260162493));
#208206=CARTESIAN_POINT('Ctrl Pts',(17.734,8.28931855664526,2.63216728166961));
#208207=CARTESIAN_POINT('Ctrl Pts',(17.734,8.26675493626269,2.64420787360863));
#208208=CARTESIAN_POINT('Ctrl Pts',(17.734,8.14790051002851,2.70763198827501));
#208209=CARTESIAN_POINT('Ctrl Pts',(17.734,8.032030238517,2.77600356619099));
#208210=CARTESIAN_POINT('Ctrl Pts',(17.734,7.91948448293877,2.84921041197833));
#208211=CARTESIAN_POINT('Ctrl Pts',(17.734,7.89990776773299,2.86194434018138));
#208212=CARTESIAN_POINT('Ctrl Pts',(17.734,7.88043170399221,2.87482465916843));
#208213=CARTESIAN_POINT('Ctrl Pts',(17.734,7.86105816656312,2.88785089183458));
#208214=CARTESIAN_POINT('Ctrl Pts',(17.734,7.74528165055074,2.96569583060084));
#208215=CARTESIAN_POINT('Ctrl Pts',(17.734,7.63316351668281,3.04874885969149));
#208216=CARTESIAN_POINT('Ctrl Pts',(17.734,7.52499462458614,3.13669681545407));
#208217=CARTESIAN_POINT('Ctrl Pts',(17.734,7.41763480848604,3.22398694271739));
#208218=CARTESIAN_POINT('Ctrl Pts',(17.734,7.31416494708026,3.31609973205607));
#208219=CARTESIAN_POINT('Ctrl Pts',(17.734,7.2149110901292,3.41275797655135));
#208220=CARTESIAN_POINT('Ctrl Pts',(17.734,7.13012408679148,3.4953276937431));
#208221=CARTESIAN_POINT('Ctrl Pts',(17.734,7.04841415789455,3.5812150691776));
#208222=CARTESIAN_POINT('Ctrl Pts',(17.734,6.97001249572361,3.67025869427777));
#208223=CARTESIAN_POINT('Ctrl Pts',(17.734,6.95431915067657,3.68808219819647));
#208224=CARTESIAN_POINT('Ctrl Pts',(17.734,6.93875844510523,3.70603218668507));
#208225=CARTESIAN_POINT('Ctrl Pts',(17.734,6.92333236973455,3.72410739902025));
#208226=CARTESIAN_POINT('Ctrl Pts',(17.734,6.91090397970631,3.7386701301976));
#208227=CARTESIAN_POINT('Ctrl Pts',(17.734,6.89856246392884,3.75331485694984));
#208228=CARTESIAN_POINT('Ctrl Pts',(17.734,6.88631933290202,3.7680280979283));
#208229=CARTESIAN_POINT('Ctrl Pts',(17.734,6.79919924774975,3.87272507487816));
#208230=CARTESIAN_POINT('Ctrl Pts',(17.734,6.7169286678634,3.98103806042143));
#208231=CARTESIAN_POINT('Ctrl Pts',(17.734,6.63977277908297,4.09267000357134));
#208232=CARTESIAN_POINT('Ctrl Pts',(17.734,6.56326133238926,4.20336954449602));
#208233=CARTESIAN_POINT('Ctrl Pts',(17.734,6.49177912371476,4.3173335019011));
#208234=CARTESIAN_POINT('Ctrl Pts',(17.734,6.42562994044659,4.43429573638148));
#208235=CARTESIAN_POINT('Ctrl Pts',(17.734,6.40600466641507,4.46899632964067));
#208236=CARTESIAN_POINT('Ctrl Pts',(17.734,6.38684913115322,4.50396095400166));
#208237=CARTESIAN_POINT('Ctrl Pts',(17.734,6.36817211518176,4.5391829311905));
#208238=CARTESIAN_POINT('Ctrl Pts',(17.734,6.30473751328733,4.65881082594215));
#208239=CARTESIAN_POINT('Ctrl Pts',(17.734,6.24681897356675,4.78140717330283));
#208240=CARTESIAN_POINT('Ctrl Pts',(17.734,6.19457219597214,4.90656879650476));
#208241=CARTESIAN_POINT('Ctrl Pts',(17.734,6.166564858854,4.97366276739939));
#208242=CARTESIAN_POINT('Ctrl Pts',(17.734,6.14018823211239,5.04149397277739));
#208243=CARTESIAN_POINT('Ctrl Pts',(17.734,6.11547251222998,5.11000011542537));
#208244=CARTESIAN_POINT('Ctrl Pts',(17.734,6.10242953316116,5.14615217528421));
#208245=CARTESIAN_POINT('Ctrl Pts',(17.734,6.08984917084278,5.18249218937426));
#208246=CARTESIAN_POINT('Ctrl Pts',(17.734,6.07773636073121,5.21901091873209));
#208247=CARTESIAN_POINT('Ctrl Pts',(17.734,6.06903436381049,5.24524643860674));
#208248=CARTESIAN_POINT('Ctrl Pts',(17.734,6.06057221985005,5.27157936583366));
#208249=CARTESIAN_POINT('Ctrl Pts',(17.734,6.05236276273648,5.29796985450767));
#208250=CARTESIAN_POINT('Ctrl Pts',(17.734,6.01297460249778,5.42458879925516));
#208251=CARTESIAN_POINT('Ctrl Pts',(17.734,5.97934462684376,5.55268880302192));
#208252=CARTESIAN_POINT('Ctrl Pts',(17.734,5.95155790703941,5.68187791678551));
#208253=CARTESIAN_POINT('Ctrl Pts',(17.734,5.92387819466376,5.81056951968859));
#208254=CARTESIAN_POINT('Ctrl Pts',(17.734,5.90199676487722,5.94034266902156));
#208255=CARTESIAN_POINT('Ctrl Pts',(17.734,5.88604904274555,6.07081358834923));
#208256=CARTESIAN_POINT('Ctrl Pts',(17.734,5.87037715515666,6.1990278602334));
#208257=CARTESIAN_POINT('Ctrl Pts',(17.734,5.8604355485385,6.3279166852093));
#208258=CARTESIAN_POINT('Ctrl Pts',(17.734,5.85640219965237,6.4571081864847));
#208259=CARTESIAN_POINT('Ctrl Pts',(17.734,5.85485839225705,6.50655761441974));
#208260=CARTESIAN_POINT('Ctrl Pts',(17.734,5.85418069613621,6.55605125001335));
#208261=CARTESIAN_POINT('Ctrl Pts',(17.734,5.85438103290403,6.60556760587704));
#208262=CARTESIAN_POINT('Ctrl Pts',(17.734,5.85480000921424,6.70912413372275));
#208263=CARTESIAN_POINT('Ctrl Pts',(17.734,5.85905829450831,6.81278078385137));
#208264=CARTESIAN_POINT('Ctrl Pts',(17.734,5.86714838588205,6.9163217216595));
#208265=CARTESIAN_POINT('Ctrl Pts',(23.534,7.33966741897454,3.77664721604216));
#208266=CARTESIAN_POINT('Ctrl Pts',(23.534,7.4278110653291,3.68403366522654));
#208267=CARTESIAN_POINT('Ctrl Pts',(23.534,7.52001976376112,3.59567730315309));
#208268=CARTESIAN_POINT('Ctrl Pts',(23.534,7.61588000351043,3.51169601948419));
#208269=CARTESIAN_POINT('Ctrl Pts',(23.534,7.71428950781667,3.42548137493008));
#208270=CARTESIAN_POINT('Ctrl Pts',(23.534,7.81654770302536,3.34387704113668));
#208271=CARTESIAN_POINT('Ctrl Pts',(23.534,7.92225677089516,3.2670337517176));
#208272=CARTESIAN_POINT('Ctrl Pts',(23.534,8.02887849234131,3.18952702533591));
#208273=CARTESIAN_POINT('Ctrl Pts',(23.534,8.13901148190336,3.11686336124311));
#208274=CARTESIAN_POINT('Ctrl Pts',(23.534,8.25229019242955,3.04922905262568));
#208275=CARTESIAN_POINT('Ctrl Pts',(23.534,8.36548868719601,2.98164263771595));
#208276=CARTESIAN_POINT('Ctrl Pts',(23.534,8.48182908274332,2.91907793777968));
#208277=CARTESIAN_POINT('Ctrl Pts',(23.534,8.60098002349002,2.86176024173783));
#208278=CARTESIAN_POINT('Ctrl Pts',(23.534,8.62551775114871,2.84995633984092));
#208279=CARTESIAN_POINT('Ctrl Pts',(23.534,8.65017477000968,2.83837511498036));
#208280=CARTESIAN_POINT('Ctrl Pts',(23.534,8.67494832377365,2.82701877421198));
#208281=CARTESIAN_POINT('Ctrl Pts',(23.534,8.69677888932777,2.81701151631264));
#208282=CARTESIAN_POINT('Ctrl Pts',(23.534,8.7187040887079,2.80717716259871));
#208283=CARTESIAN_POINT('Ctrl Pts',(23.534,8.7406954034996,2.7975286977491));
#208284=CARTESIAN_POINT('Ctrl Pts',(23.534,8.86780597067235,2.74176023410807));
#208285=CARTESIAN_POINT('Ctrl Pts',(23.534,8.99727639743939,2.69212556532351));
#208286=CARTESIAN_POINT('Ctrl Pts',(23.534,9.12866759232672,2.6487952833054));
#208287=CARTESIAN_POINT('Ctrl Pts',(23.534,9.25547643309881,2.60697617329764));
#208288=CARTESIAN_POINT('Ctrl Pts',(23.534,9.38407515938091,2.57102868262553));
#208289=CARTESIAN_POINT('Ctrl Pts',(23.534,9.51404078368099,2.54089289360578));
#208290=CARTESIAN_POINT('Ctrl Pts',(23.534,9.64599296324215,2.51029647193376));
#208291=CARTESIAN_POINT('Ctrl Pts',(23.534,9.77935483569613,2.48569051020136));
#208292=CARTESIAN_POINT('Ctrl Pts',(23.534,9.91370948271856,2.46705966806754));
#208293=CARTESIAN_POINT('Ctrl Pts',(23.534,10.031006234944,2.45079422938006));
#208294=CARTESIAN_POINT('Ctrl Pts',(23.534,10.1490603917624,2.43908365615739));
#208295=CARTESIAN_POINT('Ctrl Pts',(23.534,10.2676037380491,2.43194887296395));
#208296=CARTESIAN_POINT('Ctrl Pts',(23.534,10.3041175791339,2.42975120984864));
#208297=CARTESIAN_POINT('Ctrl Pts',(23.534,10.3406773911072,2.42798791270649));
#208298=CARTESIAN_POINT('Ctrl Pts',(23.534,10.3772769926549,2.4266601138214));
#208299=CARTESIAN_POINT('Ctrl Pts',(23.534,10.4011419710093,2.42579431500634));
#208300=CARTESIAN_POINT('Ctrl Pts',(23.534,10.4250202861952,2.42511392850954));
#208301=CARTESIAN_POINT('Ctrl Pts',(23.534,10.4488889852346,2.42461930902579));
#208302=CARTESIAN_POINT('Ctrl Pts',(23.534,10.5881947640817,2.42173254287641));
#208303=CARTESIAN_POINT('Ctrl Pts',(23.534,10.7273545088382,2.4251622122633));
#208304=CARTESIAN_POINT('Ctrl Pts',(23.534,10.8659190930214,2.43484421424554));
#208305=CARTESIAN_POINT('Ctrl Pts',(23.534,10.9998137685222,2.44419991304298));
#208306=CARTESIAN_POINT('Ctrl Pts',(23.534,11.1331535298942,2.45939375404109));
#208307=CARTESIAN_POINT('Ctrl Pts',(23.534,11.2655490821966,2.48041129060109));
#208308=CARTESIAN_POINT('Ctrl Pts',(23.534,11.2886886126467,2.48408464607836));
#208309=CARTESIAN_POINT('Ctrl Pts',(23.534,11.3117993244444,2.48793600302252));
#208310=CARTESIAN_POINT('Ctrl Pts',(23.534,11.3348791639493,2.49196542192025));
#208311=CARTESIAN_POINT('Ctrl Pts',(23.534,11.4716128752646,2.51583722571738));
#208312=CARTESIAN_POINT('Ctrl Pts',(23.534,11.6072631372987,2.54595436303442));
#208313=CARTESIAN_POINT('Ctrl Pts',(23.534,11.741474161821,2.58210348353803));
#208314=CARTESIAN_POINT('Ctrl Pts',(23.534,11.8669921985643,2.61591118787352));
#208315=CARTESIAN_POINT('Ctrl Pts',(23.534,11.9912519180839,2.65499542884546));
#208316=CARTESIAN_POINT('Ctrl Pts',(23.534,12.1139562411199,2.69922248208064));
#208317=CARTESIAN_POINT('Ctrl Pts',(23.534,12.1324792825538,2.70589885271947));
#208318=CARTESIAN_POINT('Ctrl Pts',(23.534,12.1509668598302,2.71269248793648));
#208319=CARTESIAN_POINT('Ctrl Pts',(23.534,12.1694179272643,2.71960300224709));
#208320=CARTESIAN_POINT('Ctrl Pts',(23.534,12.1864042738565,2.725964931801));
#208321=CARTESIAN_POINT('Ctrl Pts',(23.534,12.2033501584913,2.73242235622137));
#208322=CARTESIAN_POINT('Ctrl Pts',(23.534,12.2202547019028,2.73897459134067));
#208323=CARTESIAN_POINT('Ctrl Pts',(23.534,12.3523840941254,2.79018821024405));
#208324=CARTESIAN_POINT('Ctrl Pts',(23.534,12.4819900441372,2.84719066756166));
#208325=CARTESIAN_POINT('Ctrl Pts',(23.534,12.6087145787098,2.90970780354203));
#208326=CARTESIAN_POINT('Ctrl Pts',(23.534,12.7371473048524,2.97306764330525));
#208327=CARTESIAN_POINT('Ctrl Pts',(23.534,12.8626211666514,3.04209197614692));
#208328=CARTESIAN_POINT('Ctrl Pts',(23.534,12.9847605797274,3.11654906625687));
#208329=CARTESIAN_POINT('Ctrl Pts',(23.534,13.1066107532674,3.19082983380514));
#208330=CARTESIAN_POINT('Ctrl Pts',(23.534,13.2251430159627,3.27051793771162));
#208331=CARTESIAN_POINT('Ctrl Pts',(23.534,13.339970121412,3.35543295399967));
#208332=CARTESIAN_POINT('Ctrl Pts',(23.534,13.3745616920472,3.38101353249137));
#208333=CARTESIAN_POINT('Ctrl Pts',(23.534,13.4088168737746,3.40706878536305));
#208334=CARTESIAN_POINT('Ctrl Pts',(23.534,13.442724662023,3.43359460806598));
#208335=CARTESIAN_POINT('Ctrl Pts',(23.534,13.5222654936816,3.49581883757828));
#208336=CARTESIAN_POINT('Ctrl Pts',(23.534,13.5998952497886,3.56063180043892));
#208337=CARTESIAN_POINT('Ctrl Pts',(23.534,13.6755304223662,3.62791906475953));
#208338=CARTESIAN_POINT('Ctrl Pts',(23.534,13.6988785584492,3.64869025031348));
#208339=CARTESIAN_POINT('Ctrl Pts',(23.534,13.7220365683719,3.66969729110703));
#208340=CARTESIAN_POINT('Ctrl Pts',(23.534,13.7450018328666,3.69093701222324));
#208341=CARTESIAN_POINT('Ctrl Pts',(23.534,13.7616807918054,3.70636276255376));
#208342=CARTESIAN_POINT('Ctrl Pts',(23.534,13.778252633284,3.72190625726443));
#208343=CARTESIAN_POINT('Ctrl Pts',(23.534,13.794710755701,3.73756042625356));
#208344=CARTESIAN_POINT('Ctrl Pts',(23.534,13.8994714966307,3.83720376954569));
#208345=CARTESIAN_POINT('Ctrl Pts',(23.5339999999999,13.9997005890967,3.9413957803482));
#208346=CARTESIAN_POINT('Ctrl Pts',(23.5339999999999,14.0951974348199,4.04973935219108));
#208347=CARTESIAN_POINT('Ctrl Pts',(23.5339999999999,14.1919272854646,4.15948179910966));
#208348=CARTESIAN_POINT('Ctrl Pts',(23.5339999999999,14.2838024902719,4.27348416760255));
#208349=CARTESIAN_POINT('Ctrl Pts',(23.534,14.370586183448,4.39137862115632));
#208350=CARTESIAN_POINT('Ctrl Pts',(23.534,14.3939765840093,4.42315415860651));
#208351=CARTESIAN_POINT('Ctrl Pts',(23.534,14.4169969315166,4.45521265895707));
#208352=CARTESIAN_POINT('Ctrl Pts',(23.5339999999999,14.4396421540893,4.48754739858326));
#208353=CARTESIAN_POINT('Ctrl Pts',(23.5339999999999,14.4633057306723,4.52133622909603));
#208354=CARTESIAN_POINT('Ctrl Pts',(23.534,14.486559687685,4.55542670188665));
#208355=CARTESIAN_POINT('Ctrl Pts',(23.534,14.5093979973546,4.58981135573279));
#208356=CARTESIAN_POINT('Ctrl Pts',(23.5339999999999,14.5229724195575,4.6102485866559));
#208357=CARTESIAN_POINT('Ctrl Pts',(23.534,14.5363970207432,4.63078533674386));
#208358=CARTESIAN_POINT('Ctrl Pts',(23.534,14.5496664278029,4.65141310427564));
#208359=CARTESIAN_POINT('Ctrl Pts',(23.534,14.6302131840668,4.77662591568343));
#208360=CARTESIAN_POINT('Ctrl Pts',(23.5339999999999,14.7050940684627,4.90526377791114));
#208361=CARTESIAN_POINT('Ctrl Pts',(23.5339999999999,14.7740779860328,5.03693509762841));
#208362=CARTESIAN_POINT('Ctrl Pts',(23.5339999999999,14.825130242171,5.13437980904875));
#208363=CARTESIAN_POINT('Ctrl Pts',(23.534,14.8729522304357,5.2334868876652));
#208364=CARTESIAN_POINT('Ctrl Pts',(23.534,14.917437260214,5.33411057035729));
#208365=CARTESIAN_POINT('Ctrl Pts',(23.534,14.9671573568045,5.44657580299121));
#208366=CARTESIAN_POINT('Ctrl Pts',(23.5339999999999,15.012709422787,5.56093556570214));
#208367=CARTESIAN_POINT('Ctrl Pts',(23.5339999999999,15.0540735698273,5.67694764394986));
#208368=CARTESIAN_POINT('Ctrl Pts',(23.5319822588655,15.0572813588473,8.3237916645841));
#208369=CARTESIAN_POINT('Ctrl Pts',(23.4932003772294,14.8422325070833,9.12430563616661));
#208370=CARTESIAN_POINT('Ctrl Pts',(23.4156366139573,14.0148887345381,10.6178356099985));
#208371=CARTESIAN_POINT('Ctrl Pts',(23.2992909690491,11.8680999648663,12.0161880919895));
#208372=CARTESIAN_POINT('Ctrl Pts',(23.1829453241409,9.31682637793275,12.2463212706672));
#208373=CARTESIAN_POINT('Ctrl Pts',(23.0665996792327,6.95460748608732,11.2549883962344));
#208374=CARTESIAN_POINT('Ctrl Pts',(22.9502540343245,5.33172308320188,9.27285619592476));
#208375=CARTESIAN_POINT('Ctrl Pts',(22.8339083894163,4.82593288295298,6.76152807094034));
#208376=CARTESIAN_POINT('Ctrl Pts',(22.7175627445081,5.55506383184552,4.30571494350424));
#208377=CARTESIAN_POINT('Ctrl Pts',(22.6012170995999,7.3493153728942,2.47725496135783));
#208378=CARTESIAN_POINT('Ctrl Pts',(22.4848714546917,9.79091952574551,1.70188575047227));
#208379=CARTESIAN_POINT('Ctrl Pts',(22.3685258097835,12.3113588873047,2.16015052666956));
#208380=CARTESIAN_POINT('Ctrl Pts',(22.2521801648753,14.3237650772533,3.74534470495516));
#208381=CARTESIAN_POINT('Ctrl Pts',(22.1358345199671,15.3595658072703,6.08836352082835));
#208382=CARTESIAN_POINT('Ctrl Pts',(22.0194888750589,15.1775704930741,8.64365536817768));
#208383=CARTESIAN_POINT('Ctrl Pts',(21.9031432301507,13.8201792815797,10.8162233916012));
#208384=CARTESIAN_POINT('Ctrl Pts',(21.7867975852425,11.6034022891174,12.100225958688));
#208385=CARTESIAN_POINT('Ctrl Pts',(21.6704519403344,9.0435073068744,12.1966334909658));
#208386=CARTESIAN_POINT('Ctrl Pts',(21.5541062954261,6.73633029032072,11.0831185230676));
#208387=CARTESIAN_POINT('Ctrl Pts',(21.437760650518,5.21954311482696,9.01870407716815));
#208388=CARTESIAN_POINT('Ctrl Pts',(21.3214150056097,4.84535773940766,6.4846037851452));
#208389=CARTESIAN_POINT('Ctrl Pts',(21.2050693607016,5.70291518904701,4.06976343034357));
#208390=CARTESIAN_POINT('Ctrl Pts',(21.0887237157934,7.58832315778984,2.3387736849668));
#208391=CARTESIAN_POINT('Ctrl Pts',(20.9723780708852,10.0713935791024,1.68985436313296));
#208392=CARTESIAN_POINT('Ctrl Pts',(20.856032425977,12.555501431994,2.28420306077143));
#208393=CARTESIAN_POINT('Ctrl Pts',(20.7009048994327,15.1484714499262,4.5226444707105));
#208394=CARTESIAN_POINT('Ctrl Pts',(20.5069954912524,15.7229266692027,9.1400596639883));
#208395=CARTESIAN_POINT('Ctrl Pts',(20.274304201436,11.4791150714787,12.8347936062911));
#208396=CARTESIAN_POINT('Ctrl Pts',(20.0803947932557,6.98475562540071,11.6301131359937));
#208397=CARTESIAN_POINT('Ctrl Pts',(19.9252672667114,5.12461246395865,8.75366030680187));
#208398=CARTESIAN_POINT('Ctrl Pts',(19.8089216218032,4.87791900276309,6.21138090921678));
#208399=CARTESIAN_POINT('Ctrl Pts',(19.692575976895,5.86251193291384,3.84129404048311));
#208400=CARTESIAN_POINT('Ctrl Pts',(19.5762303319868,7.83658921959077,2.21215083823699));
#208401=CARTESIAN_POINT('Ctrl Pts',(19.4598846870786,10.346497559081,1.69521868991591));
#208402=CARTESIAN_POINT('Ctrl Pts',(19.3435390421704,12.8049519410314,2.41471923687709));
#208403=CARTESIAN_POINT('Ctrl Pts',(19.2271933972622,14.6408870657878,4.20127809621151));
#208404=CARTESIAN_POINT('Ctrl Pts',(19.1108477523541,15.4261618032088,6.63978685285258));
#208405=CARTESIAN_POINT('Ctrl Pts',(18.9945021074458,14.9782427651156,9.16203292881471));
#208406=CARTESIAN_POINT('Ctrl Pts',(18.8781564625377,13.4012755888355,11.1809280106677));
#208407=CARTESIAN_POINT('Ctrl Pts',(18.7618108176295,11.062518755214,12.2262888051469));
#208408=CARTESIAN_POINT('Ctrl Pts',(18.6454651727213,8.50650330604877,12.0547553007003));
#208409=CARTESIAN_POINT('Ctrl Pts',(18.5291195278131,6.32839771745935,10.7062463579064));
#208410=CARTESIAN_POINT('Ctrl Pts',(18.4127738829049,5.03535314052584,8.49476382840791));
#208411=CARTESIAN_POINT('Ctrl Pts',(18.2964282379967,4.92844964904422,5.9352340231685));
#208412=CARTESIAN_POINT('Ctrl Pts',(18.1800825930885,6.03257956786553,3.62362735793028));
#208413=CARTESIAN_POINT('Ctrl Pts',(18.0637369481803,8.09064912978604,2.09819162438962));
#208414=CARTESIAN_POINT('Ctrl Pts',(17.9473913032721,10.6234591686693,1.7141039202743));
#208415=CARTESIAN_POINT('Ctrl Pts',(17.8310456583639,13.0412397395454,2.56082098582784));
#208416=CARTESIAN_POINT('Ctrl Pts',(17.7147000134557,14.7810693674473,4.44113870113773));
#208417=CARTESIAN_POINT('Ctrl Pts',(17.5983543685475,15.4377476650143,6.9173439782558));
#208418=CARTESIAN_POINT('Ctrl Pts',(17.4820087236393,14.8585632965897,9.41264028584843));
#208419=CARTESIAN_POINT('Ctrl Pts',(17.3656591966584,13.1779145254008,11.3465351757322));
#208420=CARTESIAN_POINT('Ctrl Pts',(17.2880915513137,11.5845997651963,11.9603782329704));
#208421=CARTESIAN_POINT('Ctrl Pts',(17.2493057876049,10.7620145183404,12.0631392312232));
#208422=CARTESIAN_POINT('Ctrl Pts',(23.694570999514,14.7853120162315,8.25073023540143));
#208423=CARTESIAN_POINT('Ctrl Pts',(23.655789117878,14.5821319326992,9.00706301412011));
#208424=CARTESIAN_POINT('Ctrl Pts',(23.5782253546058,13.8004501174428,10.4181635261759));
#208425=CARTESIAN_POINT('Ctrl Pts',(23.4618797096977,11.7721448371763,11.739339490465));
#208426=CARTESIAN_POINT('Ctrl Pts',(23.3455340647894,9.36167867446536,11.9567713813296));
#208427=CARTESIAN_POINT('Ctrl Pts',(23.2291884198813,7.12983308296455,11.020151192087));
#208428=CARTESIAN_POINT('Ctrl Pts',(23.112842774973,5.59651734639213,9.14741491506193));
#208429=CARTESIAN_POINT('Ctrl Pts',(22.9964971300649,5.11864222967593,6.77468958299936));
#208430=CARTESIAN_POINT('Ctrl Pts',(22.8801514851566,5.80753168845142,4.45441531843442));
#208431=CARTESIAN_POINT('Ctrl Pts',(22.7638058402485,7.50275663384358,2.72686993113926));
#208432=CARTESIAN_POINT('Ctrl Pts',(22.6474601953403,9.80960613180611,1.99429414780511));
#208433=CARTESIAN_POINT('Ctrl Pts',(22.5311145504321,12.1909398418867,2.42726681770743));
#208434=CARTESIAN_POINT('Ctrl Pts',(22.4147689055239,14.0922792557956,3.9249724921022));
#208435=CARTESIAN_POINT('Ctrl Pts',(22.2984232606157,15.0709130737463,6.13867767965353));
#208436=CARTESIAN_POINT('Ctrl Pts',(22.1820776157075,14.8989622689056,8.5529403308379));
#208437=CARTESIAN_POINT('Ctrl Pts',(22.0657319707993,13.6164868802894,10.6056020812167));
#208438=CARTESIAN_POINT('Ctrl Pts',(21.9493863258911,11.5220560995322,11.8187392205059));
#208439=CARTESIAN_POINT('Ctrl Pts',(21.8330406809829,9.10344436522311,11.9098259215075));
#208440=CARTESIAN_POINT('Ctrl Pts',(21.7166950360747,6.92360283106935,10.8577669947277));
#208441=CARTESIAN_POINT('Ctrl Pts',(21.6003493911665,5.49052870633148,8.90728971422824));
#208442=CARTESIAN_POINT('Ctrl Pts',(21.4840037462583,5.13699500824085,6.51304903454513));
#208443=CARTESIAN_POINT('Ctrl Pts',(21.3676581013501,5.94722297654782,4.23148621297622));
#208444=CARTESIAN_POINT('Ctrl Pts',(21.251312456442,7.72857333224318,2.59603157941593));
#208445=CARTESIAN_POINT('Ctrl Pts',(21.1349668115337,10.0746005324842,1.98292678515909));
#208446=CARTESIAN_POINT('Ctrl Pts',(21.0186211666256,12.4216079073839,2.54447276433055));
#208447=CARTESIAN_POINT('Ctrl Pts',(20.8634936400813,14.8714692320025,4.65937228098899));
#208448=CARTESIAN_POINT('Ctrl Pts',(20.669584231901,15.4142196744288,9.02194756087552));
#208449=CARTESIAN_POINT('Ctrl Pts',(20.4368929420846,11.404628421799,12.5127653209751));
#208450=CARTESIAN_POINT('Ctrl Pts',(20.2429835339043,7.15831731533217,11.3745724100295));
#208451=CARTESIAN_POINT('Ctrl Pts',(20.08785600736,5.40083737612914,8.65687398328613));
#208452=CARTESIAN_POINT('Ctrl Pts',(19.9715103624518,5.16775918184238,6.25490561132425));
#208453=CARTESIAN_POINT('Ctrl Pts',(19.8551647175436,6.09801141128885,4.01562628470573));
#208454=CARTESIAN_POINT('Ctrl Pts',(19.7388190726354,7.96313733368371,2.47639717837344));
#208455=CARTESIAN_POINT('Ctrl Pts',(19.6224734277272,10.3345212396799,1.98799504920659));
#208456=CARTESIAN_POINT('Ctrl Pts',(19.506127782819,12.6572909851945,2.6677856178796));
#208457=CARTESIAN_POINT('Ctrl Pts',(19.3897821379108,14.3918989542587,4.35574244860633));
#208458=CARTESIAN_POINT('Ctrl Pts',(19.2734364930026,15.1338335678885,6.65966738847239));
#208459=CARTESIAN_POINT('Ctrl Pts',(19.1570908480944,14.7106356441191,9.04270809852214));
#208460=CARTESIAN_POINT('Ctrl Pts',(19.0407452031862,13.2207029149922,10.9501782756895));
#208461=CARTESIAN_POINT('Ctrl Pts',(18.924399558278,11.0110244864905,11.9378445282709));
#208462=CARTESIAN_POINT('Ctrl Pts',(18.8080539133698,8.59607816982169,11.7757781350949));
#208463=CARTESIAN_POINT('Ctrl Pts',(18.6917082684616,6.53818447821767,10.501694793596));
#208464=CARTESIAN_POINT('Ctrl Pts',(18.5753626235535,5.31650436694375,8.41226626892347));
#208465=CARTESIAN_POINT('Ctrl Pts',(18.4590169786453,5.21550098956712,5.99399955712194));
#208466=CARTESIAN_POINT('Ctrl Pts',(18.342671333737,6.25869283782141,3.80997285116951));
#208467=CARTESIAN_POINT('Ctrl Pts',(18.2263256888289,8.2031754150418,2.36872749123559));
#208468=CARTESIAN_POINT('Ctrl Pts',(18.1099800439207,10.5961970519886,2.00583798419682));
#208469=CARTESIAN_POINT('Ctrl Pts',(17.9936343990125,12.8805378160702,2.80582386041163));
#208470=CARTESIAN_POINT('Ctrl Pts',(17.8772887541043,14.524344449909,4.58236489901824));
#208471=CARTESIAN_POINT('Ctrl Pts',(17.7609431091961,15.1447799940149,6.92190584946314));
#208472=CARTESIAN_POINT('Ctrl Pts',(17.6445974642879,14.5975614090662,9.27948417669346));
#208473=CARTESIAN_POINT('Ctrl Pts',(17.528247937307,13.0096693793363,11.1066454102745));
#208474=CARTESIAN_POINT('Ctrl Pts',(17.4506802919623,11.5042913063256,11.6866098352056));
#208475=CARTESIAN_POINT('Ctrl Pts',(17.4118945282535,10.7271053888111,11.7836993478332));
#208476=CARTESIAN_POINT('Ctrl Pts',(23.8571597401626,14.5133426736158,8.17766880621875));
#208477=CARTESIAN_POINT('Ctrl Pts',(23.8183778585265,14.3220313583152,8.88982039207361));
#208478=CARTESIAN_POINT('Ctrl Pts',(23.7408140952544,13.5860115003476,10.2184914423533));
#208479=CARTESIAN_POINT('Ctrl Pts',(23.6244684503462,11.6761897094863,11.4624908889405));
#208480=CARTESIAN_POINT('Ctrl Pts',(23.508122805438,9.40653097099794,11.667221491992));
#208481=CARTESIAN_POINT('Ctrl Pts',(23.3917771605298,7.30505867984177,10.7853139879396));
#208482=CARTESIAN_POINT('Ctrl Pts',(23.2754315156216,5.86131160958236,9.02197363419911));
#208483=CARTESIAN_POINT('Ctrl Pts',(23.1590858707135,5.4113515763989,6.78785109505837));
#208484=CARTESIAN_POINT('Ctrl Pts',(23.0427402258052,6.0599995450573,4.60311569336461));
#208485=CARTESIAN_POINT('Ctrl Pts',(22.9263945808971,7.65619789479296,2.97648490092068));
#208486=CARTESIAN_POINT('Ctrl Pts',(22.8100489359889,9.8282927378667,2.28670254513794));
#208487=CARTESIAN_POINT('Ctrl Pts',(22.6937032910807,12.0705207964688,2.69438310874529));
#208488=CARTESIAN_POINT('Ctrl Pts',(22.5773576461725,13.8607934343379,4.10460027924924));
#208489=CARTESIAN_POINT('Ctrl Pts',(22.4610120012643,14.7822603402221,6.18899183847872));
#208490=CARTESIAN_POINT('Ctrl Pts',(22.3446663563561,14.620354044737,8.46222529349812));
#208491=CARTESIAN_POINT('Ctrl Pts',(22.2283207114479,13.4127944789992,10.3949807708323));
#208492=CARTESIAN_POINT('Ctrl Pts',(22.1119750665397,11.440709909947,11.5372524823239));
#208493=CARTESIAN_POINT('Ctrl Pts',(21.9956294216315,9.16338142357181,11.6230183520491));
#208494=CARTESIAN_POINT('Ctrl Pts',(21.8792837767233,7.11087537181799,10.6324154663879));
#208495=CARTESIAN_POINT('Ctrl Pts',(21.7629381318151,5.76151429783599,8.79587535128832));
#208496=CARTESIAN_POINT('Ctrl Pts',(21.6465924869069,5.42863227707405,6.54149428394506));
#208497=CARTESIAN_POINT('Ctrl Pts',(21.5302468419987,6.19153076404863,4.39320899560886));
#208498=CARTESIAN_POINT('Ctrl Pts',(21.4139011970905,7.86882350669652,2.85328947386507));
#208499=CARTESIAN_POINT('Ctrl Pts',(21.2975555521823,10.0778074858659,2.27599920718522));
#208500=CARTESIAN_POINT('Ctrl Pts',(21.1812099072741,12.2877143827737,2.80474246788965));
#208501=CARTESIAN_POINT('Ctrl Pts',(21.0260823807299,14.5944670140789,4.79610009126748));
#208502=CARTESIAN_POINT('Ctrl Pts',(20.8321729725495,15.105512679655,8.90383545776275));
#208503=CARTESIAN_POINT('Ctrl Pts',(20.5994816827331,11.3301417721195,12.1907370356592));
#208504=CARTESIAN_POINT('Ctrl Pts',(20.4055722745528,7.33187900526365,11.1190316840652));
#208505=CARTESIAN_POINT('Ctrl Pts',(20.2504447480086,5.6770622882996,8.56008765977039));
#208506=CARTESIAN_POINT('Ctrl Pts',(20.1340991031004,5.45759936092166,6.29843031343171));
#208507=CARTESIAN_POINT('Ctrl Pts',(20.0177534581922,6.33351088966386,4.18995852892835));
#208508=CARTESIAN_POINT('Ctrl Pts',(19.901407813284,8.08968544777665,2.74064351850989));
#208509=CARTESIAN_POINT('Ctrl Pts',(19.7850621683758,10.3225449202788,2.28077140849729));
#208510=CARTESIAN_POINT('Ctrl Pts',(19.6687165234676,12.5096300293577,2.92085199888212));
#208511=CARTESIAN_POINT('Ctrl Pts',(19.5523708785594,14.1429108427297,4.51020680100116));
#208512=CARTESIAN_POINT('Ctrl Pts',(19.4360252336512,14.841505332568,6.67954792409221));
#208513=CARTESIAN_POINT('Ctrl Pts',(19.319679588743,14.4430285231226,8.92338326822958));
#208514=CARTESIAN_POINT('Ctrl Pts',(19.2033339438348,13.040130241149,10.7194285407112));
#208515=CARTESIAN_POINT('Ctrl Pts',(19.0869882989266,10.9595302177668,11.6494002513949));
#208516=CARTESIAN_POINT('Ctrl Pts',(18.9706426540184,8.6856530335946,11.4968009694893));
#208517=CARTESIAN_POINT('Ctrl Pts',(18.8542970091102,6.74797123897598,10.2971432292856));
#208518=CARTESIAN_POINT('Ctrl Pts',(18.737951364202,5.59765559336166,8.329768709439));
#208519=CARTESIAN_POINT('Ctrl Pts',(18.6216057192938,5.50255233009001,6.05276509107539));
#208520=CARTESIAN_POINT('Ctrl Pts',(18.5052600743856,6.4848061077773,3.99631834440874));
#208521=CARTESIAN_POINT('Ctrl Pts',(18.3889144294774,8.31570170029755,2.63926335808154));
#208522=CARTESIAN_POINT('Ctrl Pts',(18.2725687845692,10.5689349353078,2.29757204811932));
#208523=CARTESIAN_POINT('Ctrl Pts',(18.1562231396611,12.7198358925949,3.05082673499542));
#208524=CARTESIAN_POINT('Ctrl Pts',(18.0398774947529,14.267619532371,4.72359109689875));
#208525=CARTESIAN_POINT('Ctrl Pts',(17.9235318498447,14.8518123230155,6.92646772067049));
#208526=CARTESIAN_POINT('Ctrl Pts',(17.8071862049365,14.3365595215429,9.14632806753851));
#208527=CARTESIAN_POINT('Ctrl Pts',(17.6908366779556,12.8414242332716,10.866755644817));
#208528=CARTESIAN_POINT('Ctrl Pts',(17.6132690326108,11.423982847455,11.4128414374409));
#208529=CARTESIAN_POINT('Ctrl Pts',(17.5744832689021,10.6921962592818,11.5042594644432));
#208530=CARTESIAN_POINT('Ctrl Pts',(24.0197484808112,14.241373331,8.10460737703607));
#208531=CARTESIAN_POINT('Ctrl Pts',(23.980966599175,14.0619307839311,8.7725777700271));
#208532=CARTESIAN_POINT('Ctrl Pts',(23.903402835903,13.3715728832524,10.0188193585307));
#208533=CARTESIAN_POINT('Ctrl Pts',(23.7870571909947,11.5802345817964,11.185642287416));
#208534=CARTESIAN_POINT('Ctrl Pts',(23.6707115460865,9.45138326753054,11.3776716026543));
#208535=CARTESIAN_POINT('Ctrl Pts',(23.5543659011784,7.48028427671899,10.5504767837922));
#208536=CARTESIAN_POINT('Ctrl Pts',(23.4380202562701,6.1261058727726,8.89653235333628));
#208537=CARTESIAN_POINT('Ctrl Pts',(23.3216746113619,5.70406092312185,6.80101260711739));
#208538=CARTESIAN_POINT('Ctrl Pts',(23.2053289664538,6.3124674016632,4.7518160682948));
#208539=CARTESIAN_POINT('Ctrl Pts',(23.0889833215455,7.80963915574233,3.2260998707021));
#208540=CARTESIAN_POINT('Ctrl Pts',(22.9726376766373,9.8469793439273,2.57911094247078));
#208541=CARTESIAN_POINT('Ctrl Pts',(22.8562920317291,11.950101751051,2.96149939978317));
#208542=CARTESIAN_POINT('Ctrl Pts',(22.7399463868209,13.6293076128802,4.28422806639629));
#208543=CARTESIAN_POINT('Ctrl Pts',(22.6236007419127,14.493607606698,6.23930599730392));
#208544=CARTESIAN_POINT('Ctrl Pts',(22.5072550970047,14.3417458205685,8.37151025615833));
#208545=CARTESIAN_POINT('Ctrl Pts',(22.3909094520964,13.209102077709,10.1843594604477));
#208546=CARTESIAN_POINT('Ctrl Pts',(22.2745638071882,11.3593637203619,11.2557657441419));
#208547=CARTESIAN_POINT('Ctrl Pts',(22.15821816228,9.22331848192051,11.3362107825909));
#208548=CARTESIAN_POINT('Ctrl Pts',(22.0418725173718,7.29814791256664,10.4070639380481));
#208549=CARTESIAN_POINT('Ctrl Pts',(21.9255268724636,6.0324998893405,8.68446098834841));
#208550=CARTESIAN_POINT('Ctrl Pts',(21.8091812275554,5.72026954590726,6.56993953334496));
#208551=CARTESIAN_POINT('Ctrl Pts',(21.6928355826472,6.43583855154944,4.55493177824152));
#208552=CARTESIAN_POINT('Ctrl Pts',(21.576489937739,8.00907368114986,3.11054736831421));
#208553=CARTESIAN_POINT('Ctrl Pts',(21.4601442928308,10.0810144392476,2.56907162921135));
#208554=CARTESIAN_POINT('Ctrl Pts',(21.3437986479226,12.1538208581636,3.06501217144877));
#208555=CARTESIAN_POINT('Ctrl Pts',(21.1886711213784,14.3174647961552,4.93282790154597));
#208556=CARTESIAN_POINT('Ctrl Pts',(20.9947617131981,14.7968056848811,8.78572335464998));
#208557=CARTESIAN_POINT('Ctrl Pts',(20.7620704233818,11.2556551224398,11.8687087503432));
#208558=CARTESIAN_POINT('Ctrl Pts',(20.5681610152013,7.50544069519511,10.8634909581011));
#208559=CARTESIAN_POINT('Ctrl Pts',(20.4130334886571,5.95328720047008,8.46330133625465));
#208560=CARTESIAN_POINT('Ctrl Pts',(20.2966878437488,5.74743954000095,6.34195501553917));
#208561=CARTESIAN_POINT('Ctrl Pts',(20.1803421988407,6.56901036803888,4.36429077315096));
#208562=CARTESIAN_POINT('Ctrl Pts',(20.0639965539325,8.21623356186958,3.00488985864633));
#208563=CARTESIAN_POINT('Ctrl Pts',(19.9476509090243,10.3105686008776,2.57354776778798));
#208564=CARTESIAN_POINT('Ctrl Pts',(19.8313052641161,12.3619690735209,3.17391837988464));
#208565=CARTESIAN_POINT('Ctrl Pts',(19.7149596192079,13.8939227312006,4.66467115339598));
#208566=CARTESIAN_POINT('Ctrl Pts',(19.5986139742997,14.5491770972477,6.69942845971203));
#208567=CARTESIAN_POINT('Ctrl Pts',(19.4822683293915,14.1754214021261,8.80405843793702));
#208568=CARTESIAN_POINT('Ctrl Pts',(19.3659226844833,12.8595575673058,10.4886788057329));
#208569=CARTESIAN_POINT('Ctrl Pts',(19.2495770395751,10.9080359490432,11.3609559745189));
#208570=CARTESIAN_POINT('Ctrl Pts',(19.1332313946669,8.77522789736752,11.2178238038838));
#208571=CARTESIAN_POINT('Ctrl Pts',(19.0168857497587,6.95775799973429,10.0925916649752));
#208572=CARTESIAN_POINT('Ctrl Pts',(18.9005401048505,5.87880681977957,8.24727114995455));
#208573=CARTESIAN_POINT('Ctrl Pts',(18.7841944599423,5.7896036706129,6.11153062502883));
#208574=CARTESIAN_POINT('Ctrl Pts',(18.6678488150341,6.71091937773318,4.18266383764797));
#208575=CARTESIAN_POINT('Ctrl Pts',(18.5515031701259,8.4282279855533,2.9097992249275));
#208576=CARTESIAN_POINT('Ctrl Pts',(18.4351575252177,10.5416728186271,2.58930611204184));
#208577=CARTESIAN_POINT('Ctrl Pts',(18.3188118803095,12.5591339691196,3.29582960957921));
#208578=CARTESIAN_POINT('Ctrl Pts',(18.2024662354013,14.0108946148327,4.86481729477925));
#208579=CARTESIAN_POINT('Ctrl Pts',(18.0861205904931,14.5588446520163,6.93102959187783));
#208580=CARTESIAN_POINT('Ctrl Pts',(17.969774945585,14.0755576340194,9.01317195838355));
#208581=CARTESIAN_POINT('Ctrl Pts',(17.8534254186041,12.6731790872071,10.6268658793594));
#208582=CARTESIAN_POINT('Ctrl Pts',(17.7758577732593,11.3436743885842,11.1390730396763));
#208583=CARTESIAN_POINT('Ctrl Pts',(17.7370720095507,10.6572871297526,11.2248195810532));
#208584=CARTESIAN_POINT('Ctrl Pts',(17.734,10.6581555755053,11.2300936493755));
#208585=CARTESIAN_POINT('Ctrl Pts',(17.734,10.7871580301293,11.2265276116833));
#208586=CARTESIAN_POINT('Ctrl Pts',(17.734,10.9158060854873,11.2169788999138));
#208587=CARTESIAN_POINT('Ctrl Pts',(17.734,11.0437268225089,11.2016549886171));
#208588=CARTESIAN_POINT('Ctrl Pts',(17.734,11.1739880981934,11.1860506989574));
#208589=CARTESIAN_POINT('Ctrl Pts',(17.7339999999999,11.3034959146602,11.1644579899871));
#208590=CARTESIAN_POINT('Ctrl Pts',(17.734,11.4318673761861,11.1370431572688));
#208591=CARTESIAN_POINT('Ctrl Pts',(17.734,11.4884530910301,11.1249587898537));
#208592=CARTESIAN_POINT('Ctrl Pts',(17.734,11.5448180845333,11.1117424890396));
#208593=CARTESIAN_POINT('Ctrl Pts',(17.734,11.6009296449061,11.0974052968746));
#208594=CARTESIAN_POINT('Ctrl Pts',(17.734,11.6231422455803,11.0917297048534));
#208595=CARTESIAN_POINT('Ctrl Pts',(17.734,11.6453151296432,11.0858784376901));
#208596=CARTESIAN_POINT('Ctrl Pts',(17.734,11.6674462597462,11.0798520970063));
#208597=CARTESIAN_POINT('Ctrl Pts',(17.734,11.6909691969026,11.0734467651264));
#208598=CARTESIAN_POINT('Ctrl Pts',(17.7339999999999,11.7144371000566,11.0668457533736));
#208599=CARTESIAN_POINT('Ctrl Pts',(17.7339999999999,11.7378417469923,11.0600519299264));
#208600=CARTESIAN_POINT('Ctrl Pts',(17.7339999999999,11.8666178352729,11.0226712332466));
#208601=CARTESIAN_POINT('Ctrl Pts',(17.734,11.9935344010332,10.9794425381218));
#208602=CARTESIAN_POINT('Ctrl Pts',(17.734,12.1181943387372,10.9305490461558));
#208603=CARTESIAN_POINT('Ctrl Pts',(17.734,12.2170317257716,10.8917835447612));
#208604=CARTESIAN_POINT('Ctrl Pts',(17.7339999999999,12.3144508717194,10.8494559613376));
#208605=CARTESIAN_POINT('Ctrl Pts',(17.734,12.4102527649422,10.8036343689628));
#208606=CARTESIAN_POINT('Ctrl Pts',(17.734,12.4582931021382,10.7806569029182));
#208607=CARTESIAN_POINT('Ctrl Pts',(17.7339999999999,12.5059267258685,10.7568005259236));
#208608=CARTESIAN_POINT('Ctrl Pts',(17.7339999999999,12.5531281105939,10.7320719318602));
#208609=CARTESIAN_POINT('Ctrl Pts',(17.7339999999999,12.5796828219838,10.7181600374899));
#208610=CARTESIAN_POINT('Ctrl Pts',(17.734,12.6061007231861,10.703972063894));
#208611=CARTESIAN_POINT('Ctrl Pts',(17.734,12.6323772088884,10.6895090305751));
#208612=CARTESIAN_POINT('Ctrl Pts',(17.734,12.6494661520011,10.6801029799934));
#208613=CARTESIAN_POINT('Ctrl Pts',(17.734,12.6664940896698,10.6705811847365));
#208614=CARTESIAN_POINT('Ctrl Pts',(17.734,12.6834496665741,10.6609498639215));
#208615=CARTESIAN_POINT('Ctrl Pts',(17.734,12.6867649951574,10.6590666491319));
#208616=CARTESIAN_POINT('Ctrl Pts',(17.7339999999999,12.6900776631735,10.6571791889994));
#208617=CARTESIAN_POINT('Ctrl Pts',(17.7339999999999,12.6933876620448,10.6552874881657));
#208618=CARTESIAN_POINT('Ctrl Pts',(17.734,12.813721983353,10.5865150973585));
#208619=CARTESIAN_POINT('Ctrl Pts',(17.7339999999999,12.9305291947834,10.5121431425042));
#208620=CARTESIAN_POINT('Ctrl Pts',(17.7339999999999,13.0435566004255,10.4326032510522));
#208621=CARTESIAN_POINT('Ctrl Pts',(17.7339999999999,13.1542860408063,10.3546804887062));
#208622=CARTESIAN_POINT('Ctrl Pts',(17.734,13.2613883832878,10.2717971251543));
#208623=CARTESIAN_POINT('Ctrl Pts',(17.734,13.3646136018082,10.184304620467));
#208624=CARTESIAN_POINT('Ctrl Pts',(17.734,13.4710521658323,10.0940885211913));
#208625=CARTESIAN_POINT('Ctrl Pts',(17.734,13.5733692644384,9.99897159633861));
#208626=CARTESIAN_POINT('Ctrl Pts',(17.734,13.6712668291685,9.89928713892361));
#208627=CARTESIAN_POINT('Ctrl Pts',(17.734,13.7691643938986,9.79960268150861));
#208628=CARTESIAN_POINT('Ctrl Pts',(17.734,13.8626431607924,9.69535014068124));
#208629=CARTESIAN_POINT('Ctrl Pts',(17.734,13.9513699801085,9.58681812087919));
#208630=CARTESIAN_POINT('Ctrl Pts',(17.734,13.9628634835586,9.57275908941993));
#208631=CARTESIAN_POINT('Ctrl Pts',(17.734,13.9742785921472,9.55862643429634));
#208632=CARTESIAN_POINT('Ctrl Pts',(17.734,13.9856099775934,9.54442644912111));
#208633=CARTESIAN_POINT('Ctrl Pts',(17.734,14.0729113490609,9.43502427702995));
#208634=CARTESIAN_POINT('Ctrl Pts',(17.734,14.155041858068,9.32188662452608));
#208635=CARTESIAN_POINT('Ctrl Pts',(17.734,14.2317472591746,9.20538350790436));
#208636=CARTESIAN_POINT('Ctrl Pts',(17.734,14.2502066068323,9.17734673993373));
#208637=CARTESIAN_POINT('Ctrl Pts',(17.734,14.2683516627921,9.14911485201464));
#208638=CARTESIAN_POINT('Ctrl Pts',(17.734,14.2861786693898,9.12069260839312));
#208639=CARTESIAN_POINT('Ctrl Pts',(17.734,14.3596274174382,9.003590603674));
#208640=CARTESIAN_POINT('Ctrl Pts',(17.734,14.4276801174426,8.88326038142579));
#208641=CARTESIAN_POINT('Ctrl Pts',(17.734,14.4902884333847,8.76012784854773));
#208642=CARTESIAN_POINT('Ctrl Pts',(17.734,14.5537529998883,8.63531131732493));
#208643=CARTESIAN_POINT('Ctrl Pts',(17.734,14.6116236543273,8.50761468833234));
#208644=CARTESIAN_POINT('Ctrl Pts',(17.734,14.6638094340128,8.37744644946211));
#208645=CARTESIAN_POINT('Ctrl Pts',(17.734,14.7100740696555,8.26204746184758));
#208646=CARTESIAN_POINT('Ctrl Pts',(17.734,14.7518702709569,8.14470509092437));
#208647=CARTESIAN_POINT('Ctrl Pts',(17.734,14.7891046475072,8.02568745899151));
#208648=CARTESIAN_POINT('Ctrl Pts',(17.734,14.7957588699923,8.0044176036614));
#208649=CARTESIAN_POINT('Ctrl Pts',(17.734,14.802267320164,7.98309421356168));
#208650=CARTESIAN_POINT('Ctrl Pts',(17.734,14.8086293625773,7.9617187827321));
#208651=CARTESIAN_POINT('Ctrl Pts',(17.734,14.8141582507119,7.94314261517331));
#208652=CARTESIAN_POINT('Ctrl Pts',(17.734,14.8195767038318,7.92452645243315));
#208653=CARTESIAN_POINT('Ctrl Pts',(17.734,14.8248800133524,7.90588690657763));
#208654=CARTESIAN_POINT('Ctrl Pts',(17.734,14.8642211214105,7.76761468527757));
#208655=CARTESIAN_POINT('Ctrl Pts',(17.734,14.8972903477015,7.62785672464352));
#208656=CARTESIAN_POINT('Ctrl Pts',(17.734,14.9240435546541,7.48706785777848));
#208657=CARTESIAN_POINT('Ctrl Pts',(17.734,14.9507706801502,7.34641624469049));
#208658=CARTESIAN_POINT('Ctrl Pts',(17.734,14.9711943919531,7.20473499473391));
#208659=CARTESIAN_POINT('Ctrl Pts',(17.734,14.9852278277044,7.06244825044858));
#208660=CARTESIAN_POINT('Ctrl Pts',(17.734,14.9897675457622,7.01641948644058));
#208661=CARTESIAN_POINT('Ctrl Pts',(17.734,14.9936381823968,6.9703271759923));
#208662=CARTESIAN_POINT('Ctrl Pts',(17.734,14.9968357553433,6.92418521713769));
#208663=CARTESIAN_POINT('Ctrl Pts',(17.734,15.0067323514289,6.78137429866483));
#208664=CARTESIAN_POINT('Ctrl Pts',(17.734,15.010185425558,6.63808849971136));
#208665=CARTESIAN_POINT('Ctrl Pts',(17.734,15.0073112040798,6.49472810706366));
#208666=CARTESIAN_POINT('Ctrl Pts',(17.734,15.0056440306924,6.41157284806935));
#208667=CARTESIAN_POINT('Ctrl Pts',(17.734,15.0018470671246,6.32839227527477));
#208668=CARTESIAN_POINT('Ctrl Pts',(17.734,14.9959350165701,6.24526375434569));
#208669=CARTESIAN_POINT('Ctrl Pts',(17.734,14.9930494071184,6.20468960101485));
#208670=CARTESIAN_POINT('Ctrl Pts',(17.734,14.9896598294849,6.16412784684823));
#208671=CARTESIAN_POINT('Ctrl Pts',(17.734,14.9857674896188,6.12358750933691));
#208672=CARTESIAN_POINT('Ctrl Pts',(17.734,14.9839181537182,6.10432590727623));
#208673=CARTESIAN_POINT('Ctrl Pts',(17.734,14.9819550242892,6.08506643814876));
#208674=CARTESIAN_POINT('Ctrl Pts',(17.734,14.9798791802301,6.06581902520355));
#208675=CARTESIAN_POINT('Ctrl Pts',(17.734,14.9642028796882,5.92046695568584));
#208676=CARTESIAN_POINT('Ctrl Pts',(17.734,14.9421349343852,5.77608373015697));
#208677=CARTESIAN_POINT('Ctrl Pts',(17.734,14.9138625332143,5.63308993321275));
#208678=CARTESIAN_POINT('Ctrl Pts',(17.734,14.8852999123965,5.48862828749952));
#208679=CARTESIAN_POINT('Ctrl Pts',(17.734,14.8504048157976,5.34558398957191));
#208680=CARTESIAN_POINT('Ctrl Pts',(17.734,14.8093178156465,5.20437943577393));
#208681=CARTESIAN_POINT('Ctrl Pts',(17.734,14.7681579286769,5.06292439032063));
#208682=CARTESIAN_POINT('Ctrl Pts',(17.734,14.7207840951535,4.9233148246561));
#208683=CARTESIAN_POINT('Ctrl Pts',(17.734,14.667285708432,4.78597583896446));
#208684=CARTESIAN_POINT('Ctrl Pts',(17.734,14.6372084702283,4.70876271833717));
#208685=CARTESIAN_POINT('Ctrl Pts',(17.734,14.6051944642011,4.63226735308866));
#208686=CARTESIAN_POINT('Ctrl Pts',(17.734,14.5712524834494,4.55656680407632));
#208687=CARTESIAN_POINT('Ctrl Pts',(17.734,14.5209818578362,4.44444859901504));
#208688=CARTESIAN_POINT('Ctrl Pts',(17.734,14.4664830452091,4.33407329976893));
#208689=CARTESIAN_POINT('Ctrl Pts',(17.734,14.4079024230562,4.22562346067727));
#208690=CARTESIAN_POINT('Ctrl Pts',(23.534,15.0539061944433,8.32288496556903));
#208691=CARTESIAN_POINT('Ctrl Pts',(23.534,15.0045196831565,8.46102105477102));
#208692=CARTESIAN_POINT('Ctrl Pts',(23.534,14.9491584466399,8.59666359933282));
#208693=CARTESIAN_POINT('Ctrl Pts',(23.534,14.8880945730864,8.72949016701669));
#208694=CARTESIAN_POINT('Ctrl Pts',(23.534,14.8263802252141,8.86373165101867));
#208695=CARTESIAN_POINT('Ctrl Pts',(23.534,14.7588406646471,8.99509750972211));
#208696=CARTESIAN_POINT('Ctrl Pts',(23.534,14.6857106710821,9.1232292879567));
#208697=CARTESIAN_POINT('Ctrl Pts',(23.534,14.6128819085716,9.25083327630936));
#208698=CARTESIAN_POINT('Ctrl Pts',(23.534,14.5345081505848,9.37523035919426));
#208699=CARTESIAN_POINT('Ctrl Pts',(23.534,14.450783174498,9.49603193123717));
#208700=CARTESIAN_POINT('Ctrl Pts',(23.534,14.3684650046542,9.61480370985814));
#208701=CARTESIAN_POINT('Ctrl Pts',(23.534,14.280973400568,9.73010024309469));
#208702=CARTESIAN_POINT('Ctrl Pts',(23.534,14.1884635407845,9.84151116501465));
#208703=CARTESIAN_POINT('Ctrl Pts',(23.534,14.1636970862173,9.87133775368834));
#208704=CARTESIAN_POINT('Ctrl Pts',(23.534,14.1385708227763,9.90088559984961));
#208705=CARTESIAN_POINT('Ctrl Pts',(23.534,14.1130874412093,9.9301462552455));
#208706=CARTESIAN_POINT('Ctrl Pts',(23.534,14.0994446628436,9.94581123421829));
#208707=CARTESIAN_POINT('Ctrl Pts',(23.534,14.0856995289216,9.96139389704753));
#208708=CARTESIAN_POINT('Ctrl Pts',(23.534,14.0718524398192,9.97689291659844));
#208709=CARTESIAN_POINT('Ctrl Pts',(23.534,14.0595282691968,9.99068733649516));
#208710=CARTESIAN_POINT('Ctrl Pts',(23.534,14.0471248899774,10.0044136985475));
#208711=CARTESIAN_POINT('Ctrl Pts',(23.534,14.0346501013912,10.0180631245397));
#208712=CARTESIAN_POINT('Ctrl Pts',(23.534,13.9325629744592,10.129762867921));
#208713=CARTESIAN_POINT('Ctrl Pts',(23.534,13.8255589167938,10.2364694610508));
#208714=CARTESIAN_POINT('Ctrl Pts',(23.534,13.7138822995671,10.3377901011926));
#208715=CARTESIAN_POINT('Ctrl Pts',(23.534,13.6072656917372,10.4345199558688));
#208716=CARTESIAN_POINT('Ctrl Pts',(23.534,13.4963893994936,10.5263409917788));
#208717=CARTESIAN_POINT('Ctrl Pts',(23.534,13.3816361432654,10.6130491512947));
#208718=CARTESIAN_POINT('Ctrl Pts',(23.534,13.2675216549389,10.6992746544493));
#208719=CARTESIAN_POINT('Ctrl Pts',(23.534,13.14957248217,10.7804443135872));
#208720=CARTESIAN_POINT('Ctrl Pts',(23.534,13.0281452130351,10.8563104469715));
#208721=CARTESIAN_POINT('Ctrl Pts',(23.534,12.9228679008957,10.9220863032682));
#208722=CARTESIAN_POINT('Ctrl Pts',(23.534,12.8149755625439,10.9838749599025));
#208723=CARTESIAN_POINT('Ctrl Pts',(23.534,12.7046950051531,11.0414837392859));
#208724=CARTESIAN_POINT('Ctrl Pts',(23.534,12.6704660549416,11.0593643892202));
#208725=CARTESIAN_POINT('Ctrl Pts',(23.534,12.6360070180388,11.0768421453942));
#208726=CARTESIAN_POINT('Ctrl Pts',(23.534,12.6013246618057,11.0939106397649));
#208727=CARTESIAN_POINT('Ctrl Pts',(23.534,12.5775343548302,11.1056187462719));
#208728=CARTESIAN_POINT('Ctrl Pts',(23.534,12.5536338344587,11.1171366062184));
#208729=CARTESIAN_POINT('Ctrl Pts',(23.534,12.5296548188552,11.1284484392924));
#208730=CARTESIAN_POINT('Ctrl Pts',(23.534,12.4026030627483,11.1883836877031));
#208731=CARTESIAN_POINT('Ctrl Pts',(23.534,12.2732186532336,11.2426060623178));
#208732=CARTESIAN_POINT('Ctrl Pts',(23.534,12.1418579788868,11.2909272251374));
#208733=CARTESIAN_POINT('Ctrl Pts',(23.534,12.0110656904147,11.3390393066126));
#208734=CARTESIAN_POINT('Ctrl Pts',(23.534,11.8783134757111,11.381301368659));
#208735=CARTESIAN_POINT('Ctrl Pts',(23.534,11.7439408942886,11.4174776418709));
#208736=CARTESIAN_POINT('Ctrl Pts',(23.534,11.7185306168275,11.4243186888322));
#208737=CARTESIAN_POINT('Ctrl Pts',(23.534,11.6930623778329,11.4309419582457));
#208738=CARTESIAN_POINT('Ctrl Pts',(23.534,11.6675384567621,11.4373456433974));
#208739=CARTESIAN_POINT('Ctrl Pts',(23.534,11.5320041155766,11.4713497936919));
#208740=CARTESIAN_POINT('Ctrl Pts',(23.534,11.394899148674,11.4991663992332));
#208741=CARTESIAN_POINT('Ctrl Pts',(23.534,11.2566535581235,11.5207487746459));
#208742=CARTESIAN_POINT('Ctrl Pts',(23.534,11.1395174117289,11.5390356239828));
#208743=CARTESIAN_POINT('Ctrl Pts',(23.534,11.0215621487013,11.5528458727715));
#208744=CARTESIAN_POINT('Ctrl Pts',(23.534,10.9030568789718,11.5621227836795));
#208745=CARTESIAN_POINT('Ctrl Pts',(23.534,10.8727885717626,11.5644922680911));
#208746=CARTESIAN_POINT('Ctrl Pts',(23.534,10.842484435087,11.5665658756357));
#208747=CARTESIAN_POINT('Ctrl Pts',(23.534,10.8121490716819,11.5683423926637));
#208748=CARTESIAN_POINT('Ctrl Pts',(23.534,10.7942046025595,11.5693932670024));
#208749=CARTESIAN_POINT('Ctrl Pts',(23.5339999999999,10.7762590661863,11.5703396029876));
#208750=CARTESIAN_POINT('Ctrl Pts',(23.534,10.7583140714215,11.5711814532735));
#208751=CARTESIAN_POINT('Ctrl Pts',(23.534,10.621315610092,11.5776084372518));
#208752=CARTESIAN_POINT('Ctrl Pts',(23.534,10.4843351016943,11.5779507199327));
#208753=CARTESIAN_POINT('Ctrl Pts',(23.534,10.3477779769602,11.5722201804618));
#208754=CARTESIAN_POINT('Ctrl Pts',(23.534,10.2117250437028,11.5665107990898));
#208755=CARTESIAN_POINT('Ctrl Pts',(23.5339999999999,10.0760915867093,11.5547732226163));
#208756=CARTESIAN_POINT('Ctrl Pts',(23.534,9.94128731881931,11.5369684475339));
#208757=CARTESIAN_POINT('Ctrl Pts',(23.534,9.80868446687355,11.5194544326505));
#208758=CARTESIAN_POINT('Ctrl Pts',(23.534,9.6768832696469,11.4960695457153));
#208759=CARTESIAN_POINT('Ctrl Pts',(23.534,9.54629292150131,11.4667302088784));
#208760=CARTESIAN_POINT('Ctrl Pts',(23.534,9.51124646542765,11.4588564280494));
#208761=CARTESIAN_POINT('Ctrl Pts',(23.534,9.47628735690692,11.4505535423166));
#208762=CARTESIAN_POINT('Ctrl Pts',(23.534,9.44142384068048,11.4418193834442));
#208763=CARTESIAN_POINT('Ctrl Pts',(23.534,9.35465567581843,11.4200818475038));
#208764=CARTESIAN_POINT('Ctrl Pts',(23.534,9.26847914064439,11.395673426388));
#208765=CARTESIAN_POINT('Ctrl Pts',(23.534,9.18301437324067,11.3686311001959));
#208766=CARTESIAN_POINT('Ctrl Pts',(23.5339999999999,9.15095469784315,11.3584869410757));
#208767=CARTESIAN_POINT('Ctrl Pts',(23.534,9.11899524917183,11.347972079119));
#208768=CARTESIAN_POINT('Ctrl Pts',(23.534,9.08714263326126,11.3370882239502));
#208769=CARTESIAN_POINT('Ctrl Pts',(23.534,9.06138445704345,11.328286803679));
#208770=CARTESIAN_POINT('Ctrl Pts',(23.534,9.03570611685647,11.3192474073759));
#208771=CARTESIAN_POINT('Ctrl Pts',(23.534,9.01012249887741,11.3099758407481));
#208772=CARTESIAN_POINT('Ctrl Pts',(23.534,8.88381687735452,11.2642023701475));
#208773=CARTESIAN_POINT('Ctrl Pts',(23.534,8.75972821578054,11.2127431095304));
#208774=CARTESIAN_POINT('Ctrl Pts',(23.534,8.63823633686677,11.1557838962941));
#208775=CARTESIAN_POINT('Ctrl Pts',(23.534,8.51762502970603,11.099237522786));
#208776=CARTESIAN_POINT('Ctrl Pts',(23.534,8.39957237008985,11.0372701269964));
#208777=CARTESIAN_POINT('Ctrl Pts',(23.534,8.28448331186548,10.9700247931754));
#208778=CARTESIAN_POINT('Ctrl Pts',(23.534,8.26743565831103,10.9600640273839));
#208779=CARTESIAN_POINT('Ctrl Pts',(23.534,8.25045309970698,10.9499873952506));
#208780=CARTESIAN_POINT('Ctrl Pts',(23.534,8.23353702790625,10.939795299223));
#208781=CARTESIAN_POINT('Ctrl Pts',(23.534,8.20315452082413,10.9214895463633));
#208782=CARTESIAN_POINT('Ctrl Pts',(23.534,8.17298647883075,10.902811329405));
#208783=CARTESIAN_POINT('Ctrl Pts',(23.534,8.14304114129207,10.8837628607093));
#208784=CARTESIAN_POINT('Ctrl Pts',(23.534,8.12583577094011,10.8728183870288));
#208785=CARTESIAN_POINT('Ctrl Pts',(23.534,8.1087059434679,10.8617529204478));
#208786=CARTESIAN_POINT('Ctrl Pts',(23.534,8.09166038518003,10.8505717991687));
#208787=CARTESIAN_POINT('Ctrl Pts',(23.534,7.98236466033437,10.778878708561));
#208788=CARTESIAN_POINT('Ctrl Pts',(23.534,7.87644328077357,10.7023783007896));
#208789=CARTESIAN_POINT('Ctrl Pts',(23.534,7.77426954147463,10.6212231772217));
#208790=CARTESIAN_POINT('Ctrl Pts',(23.534,7.70156836402746,10.5634776833234));
#208791=CARTESIAN_POINT('Ctrl Pts',(23.534,7.6307652650132,10.5033747155762));
#208792=CARTESIAN_POINT('Ctrl Pts',(23.534,7.56200744420826,10.4409593356367));
#208793=CARTESIAN_POINT('Ctrl Pts',(23.534,7.4852823732511,10.3713116301304));
#208794=CARTESIAN_POINT('Ctrl Pts',(23.534,7.41110370365363,10.298784417752));
#208795=CARTESIAN_POINT('Ctrl Pts',(23.534,7.33961515870573,10.2235362531339));
#208796=CARTESIAN_POINT('Ctrl Pts',(-17.1175857387455,20.5721719462546,
0.0021420622487661));
#208797=CARTESIAN_POINT('Ctrl Pts',(-16.6641680440313,20.0337688721201,
0.0445526553076218));
#208798=CARTESIAN_POINT('Ctrl Pts',(-16.3459143283547,18.477787514409,0.129355183926955));
#208799=CARTESIAN_POINT('Ctrl Pts',(-18.0613963234494,16.802775720219,0.256549648106768));
#208800=CARTESIAN_POINT('Ctrl Pts',(-20.3933471209293,17.343653714663,0.383725454788201));
#208801=CARTESIAN_POINT('Ctrl Pts',(-21.203092243631,19.5945946034862,0.510901261469636));
#208802=CARTESIAN_POINT('Ctrl Pts',(-19.7475288885744,21.4952120560344,
0.638077068151069));
#208803=CARTESIAN_POINT('Ctrl Pts',(-17.3621513494713,21.2993774656764,
0.765252874832505));
#208804=CARTESIAN_POINT('Ctrl Pts',(-16.2353413405934,19.1880163469751,
0.892428681513937));
#208805=CARTESIAN_POINT('Ctrl Pts',(-17.4009051420832,17.0975180849442,
1.01960448819538));
#208806=CARTESIAN_POINT('Ctrl Pts',(-19.7894957664261,16.9461241370553,
1.14678029487681));
#208807=CARTESIAN_POINT('Ctrl Pts',(-21.2097371145961,18.8725531087288,
1.27395610155824));
#208808=CARTESIAN_POINT('Ctrl Pts',(-20.358641983851,21.1095172903669,1.40113190823968));
#208809=CARTESIAN_POINT('Ctrl Pts',(-18.0170393638345,21.6046935058561,
1.52830771492111));
#208810=CARTESIAN_POINT('Ctrl Pts',(-16.333203267628,19.9038128993918,1.65548352160254));
#208811=CARTESIAN_POINT('Ctrl Pts',(-16.8519493500829,17.5673150993311,
1.78265932828398));
#208812=CARTESIAN_POINT('Ctrl Pts',(-19.0973599935786,16.7387984392048,
1.90983513496541));
#208813=CARTESIAN_POINT('Ctrl Pts',(-21.0094104459781,18.1783720950554,
2.03701094164685));
#208814=CARTESIAN_POINT('Ctrl Pts',(-20.8339130159653,20.5653183707664,
2.16418674832828));
#208815=CARTESIAN_POINT('Ctrl Pts',(-18.7318757426636,21.7097612836464,
2.29136255500972));
#208816=CARTESIAN_POINT('Ctrl Pts',(-16.6317873365857,20.561745973449,2.41853836169115));
#208817=CARTESIAN_POINT('Ctrl Pts',(-16.4603485748086,18.1745049842297,
2.54571416837258));
#208818=CARTESIAN_POINT('Ctrl Pts',(-18.3748438750272,16.7381838840222,
2.67288997505402));
#208819=CARTESIAN_POINT('Ctrl Pts',(-20.6188426291484,17.5705180670209,
2.80006578173545));
#208820=CARTESIAN_POINT('Ctrl Pts',(-21.1336152570428,19.9078926156331,
2.92724158841689));
#208821=CARTESIAN_POINT('Ctrl Pts',(-19.4468898237851,21.6059114372621,
3.05441739509832));
#208822=CARTESIAN_POINT('Ctrl Pts',(-17.1061322239997,21.1067476633747,
3.18159320177976));
#208823=CARTESIAN_POINT('Ctrl Pts',(-16.2588422718968,18.8683530700484,
3.30876900846119));
#208824=CARTESIAN_POINT('Ctrl Pts',(-17.6823559096773,16.9443157687486,
3.43594481514263));
#208825=CARTESIAN_POINT('Ctrl Pts',(-20.0706877279544,17.0998205628843,
3.56312062182406));
#208826=CARTESIAN_POINT('Ctrl Pts',(-21.2326915200203,19.1922014562322,
3.6902964285055));
#208827=CARTESIAN_POINT('Ctrl Pts',(-20.102300928759,21.3018288465973,3.81747223518693));
#208828=CARTESIAN_POINT('Ctrl Pts',(-17.7165791616921,21.4932505417456,
3.94464804186836));
#208829=CARTESIAN_POINT('Ctrl Pts',(-16.264277865515,19.590849017254,4.0718238485498));
#208830=CARTESIAN_POINT('Ctrl Pts',(-17.0777933394838,17.3399595955375,
4.19899965523123));
#208831=CARTESIAN_POINT('Ctrl Pts',(-19.4107756286979,16.8056336150422,
4.32617546191267));
#208832=CARTESIAN_POINT('Ctrl Pts',(-21.1228582840144,18.4780819988752,
4.4533512685941));
#208833=CARTESIAN_POINT('Ctrl Pts',(-20.6433117330145,20.8229371587163,
4.58052707527553));
#208834=CARTESIAN_POINT('Ctrl Pts',(-18.4120901722247,21.6889400235399,
4.70770288195697));
#208835=CARTESIAN_POINT('Ctrl Pts',(-16.4762008984415,20.281586715068,4.8348786886384));
#208836=CARTESIAN_POINT('Ctrl Pts',(-16.6117021655217,17.8920365436271,
4.96205449531983));
#208837=CARTESIAN_POINT('Ctrl Pts',(-18.6942799710763,16.7125534793035,
5.08923030200127));
#208838=CARTESIAN_POINT('Ctrl Pts',(-20.8132984378653,17.8252400266391,
5.21640610868271));
#208839=CARTESIAN_POINT('Ctrl Pts',(-21.0246896437286,20.2092753395693,
5.34358191536413));
#208840=CARTESIAN_POINT('Ctrl Pts',(-19.1345152777048,21.6774549884001,
5.47075772204558));
#208841=CARTESIAN_POINT('Ctrl Pts',(-16.8768930031683,20.8828152708351,
5.59793352872701));
#208842=CARTESIAN_POINT('Ctrl Pts',(-16.3230511331653,18.5543888068372,
5.72510933540844));
#208843=CARTESIAN_POINT('Ctrl Pts',(-17.98110520812,16.8283623586792,5.85228514208988));
#208844=CARTESIAN_POINT('Ctrl Pts',(-20.3298935247037,17.288258063263,5.97946094877131));
#208845=CARTESIAN_POINT('Ctrl Pts',(-21.2145485846948,19.5121501559794,
6.10663675545275));
#208846=CARTESIAN_POINT('Ctrl Pts',(-19.8234542784372,21.4597556720715,
6.23381256213418));
#208847=CARTESIAN_POINT('Ctrl Pts',(-17.4328532908718,21.3442674325558,
6.36098836881561));
#208848=CARTESIAN_POINT('Ctrl Pts',(-16.235973650659,19.2716387291798,6.48816417549706));
#208849=CARTESIAN_POINT('Ctrl Pts',(-17.3308781409654,17.1433777554452,
6.61533998217847));
#208850=CARTESIAN_POINT('Ctrl Pts',(-19.7130598493718,16.9120318599802,
6.74251578885992));
#208851=CARTESIAN_POINT('Ctrl Pts',(-21.1970149132871,18.7898465429281,
6.86969159554135));
#208852=CARTESIAN_POINT('Ctrl Pts',(-20.4213066662076,21.054043383008,6.99686740222279));
#208853=CARTESIAN_POINT('Ctrl Pts',(-18.0975992789452,21.6273623113514,
7.12404320890422));
#208854=CARTESIAN_POINT('Ctrl Pts',(-16.3577500537671,19.9838187953891,
7.25121901558565));
#208855=CARTESIAN_POINT('Ctrl Pts',(-16.7979626675525,17.6312620012014,
7.37839482226709));
#208856=CARTESIAN_POINT('Ctrl Pts',(-19.0143693698296,16.7280167713133,
7.50557062894852));
#208857=CARTESIAN_POINT('Ctrl Pts',(-20.9735545769736,18.1027545424254,
7.63274643562996));
#208858=CARTESIAN_POINT('Ctrl Pts',(-20.8780874621779,20.4942387353917,
7.75992224231139));
#208859=CARTESIAN_POINT('Ctrl Pts',(-18.8155531779101,21.7084310354144,
7.88709804899282));
#208860=CARTESIAN_POINT('Ctrl Pts',(-16.6781989146708,20.6313853684961,
8.01427385567426));
#208861=CARTESIAN_POINT('Ctrl Pts',(-16.4269145498154,18.2512242850411,
8.1414496623557));
#208862=CARTESIAN_POINT('Ctrl Pts',(-18.2922378916319,16.7515978496617,
8.26862546903713));
#208863=CARTESIAN_POINT('Ctrl Pts',(-20.5628505490275,17.5083202395048,
8.39580127571856));
#208864=CARTESIAN_POINT('Ctrl Pts',(-21.155606338957,19.8271456293778,8.5229770824));
#208865=CARTESIAN_POINT('Ctrl Pts',(-19.5266886147337,21.5806956466074,
8.65015288908143));
#208866=CARTESIAN_POINT('Ctrl Pts',(-17.1705282862964,21.160196987974,8.77732869576286));
#208867=CARTESIAN_POINT('Ctrl Pts',(-16.2487562151834,18.9514310736836,
8.9045045024443));
#208868=CARTESIAN_POINT('Ctrl Pts',(-17.607041065014,16.9808035386242,9.03168030912573));
#208869=CARTESIAN_POINT('Ctrl Pts',(-19.9992407907343,17.0562428352734,
9.15885611580717));
#208870=CARTESIAN_POINT('Ctrl Pts',(-21.2306606206557,19.1085380912468,
9.2860319224886));
#208871=CARTESIAN_POINT('Ctrl Pts',(-20.1715492913599,21.2548357889979,
9.41320772917003));
#208872=CARTESIAN_POINT('Ctrl Pts',(-17.7935757116131,21.5260410050991,
9.54038353585147));
#208873=CARTESIAN_POINT('Ctrl Pts',(-16.278383047147,19.6733397866716,9.66755934253291));
#208874=CARTESIAN_POINT('Ctrl Pts',(-17.0160665241465,17.3964705100163,
9.79473514921434));
#208875=CARTESIAN_POINT('Ctrl Pts',(-19.3298473382648,16.7843194180195,
9.92191095589577));
#208876=CARTESIAN_POINT('Ctrl Pts',(-21.0969752019817,18.3984971432064,
10.0490867625772));
#208877=CARTESIAN_POINT('Ctrl Pts',(-20.696219980662,20.7580958098868,10.1762625692586));
#208878=CARTESIAN_POINT('Ctrl Pts',(-18.4952497161921,21.6983300945914,
10.3034383759401));
#208879=CARTESIAN_POINT('Ctrl Pts',(-16.5133180186021,20.356593398625,10.4306141826215));
#208880=CARTESIAN_POINT('Ctrl Pts',(-16.5687242078764,17.9638458629655,
10.5577899893029));
#208881=CARTESIAN_POINT('Ctrl Pts',(-18.6106365442519,16.7152848409195,
10.6849657959844));
#208882=CARTESIAN_POINT('Ctrl Pts',(-20.7657271944765,17.7563875757774,
10.8121416026658));
#208883=CARTESIAN_POINT('Ctrl Pts',(-21.0568342469805,20.1320069264304,
10.9393174093472));
#208884=CARTESIAN_POINT('Ctrl Pts',(-19.2168850492326,21.6626595862203,
11.0664932160287));
#208885=CARTESIAN_POINT('Ctrl Pts',(-16.93391879004,20.9440667428082,11.1936690227101));
#208886=CARTESIAN_POINT('Ctrl Pts',(-16.3024153153455,18.6354927291228,
11.3208448293915));
#208887=CARTESIAN_POINT('Ctrl Pts',(-17.9017398676552,16.8549109164576,
11.448020636073));
#208888=CARTESIAN_POINT('Ctrl Pts',(-20.2646114355015,17.2358946025617,
11.5751964427544));
#208889=CARTESIAN_POINT('Ctrl Pts',(-21.2232420117351,19.428914901949,11.7023722494359));
#208890=CARTESIAN_POINT('Ctrl Pts',(-19.8981475419851,21.4220118041223,
11.8295480561173));
#208891=CARTESIAN_POINT('Ctrl Pts',(-17.5050199576091,21.3866426068827,
11.9567238627987));
#208892=CARTESIAN_POINT('Ctrl Pts',(-16.2394052830226,19.3552563534375,
12.0838996694802));
#208893=CARTESIAN_POINT('Ctrl Pts',(-17.2624264292529,17.1915238492725,
12.2110754761616));
#208894=CARTESIAN_POINT('Ctrl Pts',(-19.635524990487,16.880535370574,12.338251282843));
#208895=CARTESIAN_POINT('Ctrl Pts',(-21.1815303279007,18.707603544426,12.4654270895244));
#208896=CARTESIAN_POINT('Ctrl Pts',(-20.48207850033,20.9965067219594,12.5926028962059));
#208897=CARTESIAN_POINT('Ctrl Pts',(-18.1788731466945,21.6473183031405,
12.7197787028873));
#208898=CARTESIAN_POINT('Ctrl Pts',(-16.3849622259084,20.0629590561579,
12.8469545095688));
#208899=CARTESIAN_POINT('Ctrl Pts',(-16.7461476651242,17.6969802536931,
12.9741303162502));
#208900=CARTESIAN_POINT('Ctrl Pts',(-18.9310642415578,16.7200205978014,
13.1013061229316));
#208901=CARTESIAN_POINT('Ctrl Pts',(-20.9351866075484,18.0283799358088,
13.2284819296131));
#208902=CARTESIAN_POINT('Ctrl Pts',(-20.9198568821621,20.4217197810322,
13.3556577362945));
#208903=CARTESIAN_POINT('Ctrl Pts',(-18.8991391369708,21.7042993729031,
13.4828335429759));
#208904=CARTESIAN_POINT('Ctrl Pts',(-16.7269164832995,20.6994315417472,
13.6100093496574));
#208905=CARTESIAN_POINT('Ctrl Pts',(-16.3960683825486,18.3290201535185,
13.7371851563388));
#208906=CARTESIAN_POINT('Ctrl Pts',(-18.2101274324079,16.7677705325936,
13.8643609630202));
#208907=CARTESIAN_POINT('Ctrl Pts',(-20.5048070478343,17.4480323040911,
13.9915367697017));
#208908=CARTESIAN_POINT('Ctrl Pts',(-21.1748811055536,19.7457075144692,
14.1187125763831));
#208909=CARTESIAN_POINT('Ctrl Pts',(-19.6055982470946,21.5528217680131,
14.2458883830645));
#208910=CARTESIAN_POINT('Ctrl Pts',(-17.2366780944146,21.2114598992563,
14.373064189746));
#208911=CARTESIAN_POINT('Ctrl Pts',(-16.2414578558307,19.0348002354761,
14.5002399964274));
#208912=CARTESIAN_POINT('Ctrl Pts',(-17.5329903299092,17.0197929194559,
14.6274158031088));
#208913=CARTESIAN_POINT('Ctrl Pts',(-19.926374633229,17.0150820981853,14.7545916097903));
#208914=CARTESIAN_POINT('Ctrl Pts',(-21.2258292176773,19.0249896577937,
14.8817674164717));
#208915=CARTESIAN_POINT('Ctrl Pts',(-20.2391851552704,21.2055501612724,
15.0089432231531));
#208916=CARTESIAN_POINT('Ctrl Pts',(-17.8716271352296,21.5562346875283,
15.1361190298346));
#208917=CARTESIAN_POINT('Ctrl Pts',(-16.2952426937192,19.7553119496581,
15.263294836516));
#208918=CARTESIAN_POINT('Ctrl Pts',(-16.956266714372,17.4550167817861,15.3904706431974));
#208919=CARTESIAN_POINT('Ctrl Pts',(-19.2482506860169,16.7657272280153,
15.5176464498789));
#208920=CARTESIAN_POINT('Ctrl Pts',(-21.0684415712385,18.3198236717957,
15.6448222565603));
#208921=CARTESIAN_POINT('Ctrl Pts',(-20.7469272066335,20.6915190840625,
15.7719980632418));
#208922=CARTESIAN_POINT('Ctrl Pts',(-18.5786770662948,21.7049301280798,
15.8991738699232));
#208923=CARTESIAN_POINT('Ctrl Pts',(-16.5529260772022,20.4303150703447,
16.0263496766046));
#208924=CARTESIAN_POINT('Ctrl Pts',(-16.5281750395616,18.0370541147968,
16.153525483286));
#208925=CARTESIAN_POINT('Ctrl Pts',(-18.5271314941859,16.7208156456237,
16.2807012899675));
#208926=CARTESIAN_POINT('Ctrl Pts',(-20.7158769631869,17.689166763319,16.4078770966489));
#208927=CARTESIAN_POINT('Ctrl Pts',(-21.0863733276212,20.0537054200458,
16.5350529033304));
#208928=CARTESIAN_POINT('Ctrl Pts',(-19.2987131687179,21.6451141580778,
16.6622287100118));
#208929=CARTESIAN_POINT('Ctrl Pts',(-16.9929637275681,21.0033742342365,
16.7894045166932));
#208930=CARTESIAN_POINT('Ctrl Pts',(-16.2845070054764,18.7172421977746,
16.9165803233747));
#208931=CARTESIAN_POINT('Ctrl Pts',(-17.8233080731787,16.884102298789,17.0437561300561));
#208932=CARTESIAN_POINT('Ctrl Pts',(-20.1976124598239,17.1857466171053,
17.1709319367376));
#208933=CARTESIAN_POINT('Ctrl Pts',(-21.2291432566148,19.3454352128261,
17.2981077434189));
#208934=CARTESIAN_POINT('Ctrl Pts',(-19.9715349815179,21.3817878447692,
17.4252835501004));
#208935=CARTESIAN_POINT('Ctrl Pts',(-17.5785651709616,21.4265773634257,
17.5524593567818));
#208936=CARTESIAN_POINT('Ctrl Pts',(-16.245635101675,19.4387121653785,17.6796351634633));
#208937=CARTESIAN_POINT('Ctrl Pts',(-17.195625381257,17.2419351890085,17.8068109701447));
#208938=CARTESIAN_POINT('Ctrl Pts',(-19.5569788912398,16.8516529627759,
17.9339867768261));
#208939=CARTESIAN_POINT('Ctrl Pts',(-21.1633003483382,18.6259252056079,
18.0611625835076));
#208940=CARTESIAN_POINT('Ctrl Pts',(-20.5408895152254,20.9369672584502,
18.188338390189));
#208941=CARTESIAN_POINT('Ctrl Pts',(-18.2607697000954,21.6645414772881,
18.3155141968704));
#208942=CARTESIAN_POINT('Ctrl Pts',(-16.4148093131604,20.1411436746453,
18.4426900035519));
#208943=CARTESIAN_POINT('Ctrl Pts',(-16.696562436159,17.7643967817956,18.5698658102333));
#208944=CARTESIAN_POINT('Ctrl Pts',(-18.8475380664095,16.7148185552248,
18.6970416169147));
#208945=CARTESIAN_POINT('Ctrl Pts',(-20.8943495675715,17.9553318739381,
18.8242174235962));
#208946=CARTESIAN_POINT('Ctrl Pts',(-20.9591744271437,20.3478427623818,
18.9513932302776));
#208947=CARTESIAN_POINT('Ctrl Pts',(-18.9825398592484,21.6973709774882,
19.078569036959));
#208948=CARTESIAN_POINT('Ctrl Pts',(-16.77788539751,20.7658081409326,19.2057448436405));
#208949=CARTESIAN_POINT('Ctrl Pts',(-16.3678446716688,18.4078053400529,
19.3329206503219));
#208950=CARTESIAN_POINT('Ctrl Pts',(-18.1286046027284,16.7866837825795,
19.4600964570034));
#208951=CARTESIAN_POINT('Ctrl Pts',(-20.4447772293123,17.3897218945994,
19.5872722636848));
#208952=CARTESIAN_POINT('Ctrl Pts',(-21.1914179431377,19.6636696077008,
19.7144480703662));
#208953=CARTESIAN_POINT('Ctrl Pts',(-19.683530194942,21.5223210888799,19.8416238770476));
#208954=CARTESIAN_POINT('Ctrl Pts',(-17.3045074731465,21.260478855902,19.9687996837291));
#208955=CARTESIAN_POINT('Ctrl Pts',(-16.2369553322288,19.118367116143,20.0959754904105));
#208956=CARTESIAN_POINT('Ctrl Pts',(-17.4602868598788,17.0612400309757,
20.223151297092));
#208957=CARTESIAN_POINT('Ctrl Pts',(-19.8521708105233,16.9763848025611,
20.3503271037734));
#208958=CARTESIAN_POINT('Ctrl Pts',(-21.2182030751438,18.9416493308234,
20.4775029104549));
#208959=CARTESIAN_POINT('Ctrl Pts',(-20.305131989166,21.154028290157,20.6046787171362));
#208960=CARTESIAN_POINT('Ctrl Pts',(-17.9506471621875,21.5837957108187,
20.7318545238177));
#208961=CARTESIAN_POINT('Ctrl Pts',(-16.3148354273652,19.8366774312875,
20.8590303304991));
#208962=CARTESIAN_POINT('Ctrl Pts',(-16.8984657403956,17.5155252757358,
20.9862061371806));
#208963=CARTESIAN_POINT('Ctrl Pts',(-19.1660680401668,16.7498922826988,
21.113381943862));
#208964=CARTESIAN_POINT('Ctrl Pts',(-21.0373070469929,18.2421221167019,
21.2405577505435));
#208965=CARTESIAN_POINT('Ctrl Pts',(-20.7953425225475,20.6233350697589,
21.3677335572248));
#208966=CARTESIAN_POINT('Ctrl Pts',(-18.6623441810672,21.7086297969706,
21.4949093639063));
#208967=CARTESIAN_POINT('Ctrl Pts',(-16.5948543422637,20.502867400276,21.6220851705877));
#208968=CARTESIAN_POINT('Ctrl Pts',(-16.4903436183303,18.1111966683195,
21.7492609772692));
#208969=CARTESIAN_POINT('Ctrl Pts',(-18.4433885098624,16.7298792897364,
21.8764367839506));
#208970=CARTESIAN_POINT('Ctrl Pts',(-20.6647168984764,17.6222041838633,
22.003612590632));
#208971=CARTESIAN_POINT('Ctrl Pts',(-21.1114420608105,19.9774734447106,
22.1307883973135));
#208972=CARTESIAN_POINT('Ctrl Pts',(-19.9599075668543,21.0705044715179,
22.2155722684344));
#208973=CARTESIAN_POINT('Ctrl Pts',(-19.2802415985968,21.2523731445725,
22.2579642039949));
#208974=CARTESIAN_POINT('Ctrl Pts',(-17.0028273852109,20.6688092100886,
-0.0844763361257089));
#208975=CARTESIAN_POINT('Ctrl Pts',(-16.5172190142843,20.092181868941,-0.0420657430668533));
#208976=CARTESIAN_POINT('Ctrl Pts',(-16.1763706746349,18.4257326299315,
0.0427367855524802));
#208977=CARTESIAN_POINT('Ctrl Pts',(-18.01364439973,16.6318023132686,0.169931249732293));
#208978=CARTESIAN_POINT('Ctrl Pts',(-20.5111535200096,17.2110802832593,
0.297107056413727));
#208979=CARTESIAN_POINT('Ctrl Pts',(-21.3783870101994,19.6218281451444,
0.424282863095161));
#208980=CARTESIAN_POINT('Ctrl Pts',(-19.8194850134989,21.6573811366705,
0.551458669776596));
#208981=CARTESIAN_POINT('Ctrl Pts',(-17.2647560862599,21.4476431456228,
0.678634476458029));
#208982=CARTESIAN_POINT('Ctrl Pts',(-16.057947487624,19.1863846079818,0.805810283139464));
#208983=CARTESIAN_POINT('Ctrl Pts',(-17.3062612289062,16.947470098725,0.932986089820897));
#208984=CARTESIAN_POINT('Ctrl Pts',(-19.8644313564053,16.7853278416859,
1.06016189650233));
#208985=CARTESIAN_POINT('Ctrl Pts',(-21.3855036379843,18.848524857474,1.18733770318377));
#208986=CARTESIAN_POINT('Ctrl Pts',(-20.4739844697589,21.2443037270014,
1.3145135098652));
#208987=CARTESIAN_POINT('Ctrl Pts',(-17.9661382896929,21.774635291315,1.44168931654664));
#208988=CARTESIAN_POINT('Ctrl Pts',(-16.1627571841069,19.9529995896776,
1.56886512322807));
#208989=CARTESIAN_POINT('Ctrl Pts',(-16.7183319730092,17.4506206494911,
1.69604092990951));
#208990=CARTESIAN_POINT('Ctrl Pts',(-19.1231569662995,16.5632829246964,
1.82321673659094));
#208991=CARTESIAN_POINT('Ctrl Pts',(-21.1709546507375,18.1050600233756,
1.95039254327237));
#208992=CARTESIAN_POINT('Ctrl Pts',(-20.9829976696055,20.6614690606707,
2.07756834995381));
#208993=CARTESIAN_POINT('Ctrl Pts',(-18.7317249296694,21.8871624224886,
2.20474415663524));
#208994=CARTESIAN_POINT('Ctrl Pts',(-16.4825394180193,20.6576430387449,
2.33191996331668));
#208995=CARTESIAN_POINT('Ctrl Pts',(-16.2989292528432,18.1009183645693,
2.45909576999811));
#208996=CARTESIAN_POINT('Ctrl Pts',(-18.3493453586185,16.5626247387795,
2.58627157667954));
#208997=CARTESIAN_POINT('Ctrl Pts',(-20.7526582245547,17.4540510138992,
2.71344738336098));
#208998=CARTESIAN_POINT('Ctrl Pts',(-21.3039774609752,19.9573689479556,
2.84062319004241));
#208999=CARTESIAN_POINT('Ctrl Pts',(-19.4975018880252,21.7759396905319,
2.96779899672385));
#209000=CARTESIAN_POINT('Ctrl Pts',(-16.9905607209365,21.2413374685879,
3.09497480340528));
#209001=CARTESIAN_POINT('Ctrl Pts',(-16.0831168824194,18.8440266343892,
3.22215061008672));
#209002=CARTESIAN_POINT('Ctrl Pts',(-17.6076937718807,16.7833910871266,
3.34932641676815));
#209003=CARTESIAN_POINT('Ctrl Pts',(-20.1655867192137,16.9499360425438,
3.47650222344959));
#209004=CARTESIAN_POINT('Ctrl Pts',(-21.4100877059499,19.1908668417195,
3.60367803013102));
#209005=CARTESIAN_POINT('Ctrl Pts',(-20.1994443192179,21.4502685638837,
3.73085383681246));
#209006=CARTESIAN_POINT('Ctrl Pts',(-17.6443467253329,21.6552803634332,
3.85802964349388));
#209007=CARTESIAN_POINT('Ctrl Pts',(-16.0889383794468,19.6178166386469,
3.98520545017533));
#209008=CARTESIAN_POINT('Ctrl Pts',(-16.9602098993781,17.2071238978084,
4.11238125685675));
#209009=CARTESIAN_POINT('Ctrl Pts',(-19.4588237428005,16.6348631061435,
4.23955706353819));
#209010=CARTESIAN_POINT('Ctrl Pts',(-21.2924567898383,18.4260480215086,
4.36673287021963));
#209011=CARTESIAN_POINT('Ctrl Pts',(-20.7788645279368,20.9373776575228,
4.49390867690106));
#209012=CARTESIAN_POINT('Ctrl Pts',(-18.3892359802594,21.8648629438428,
4.62108448358249));
#209013=CARTESIAN_POINT('Ctrl Pts',(-16.3159070222257,20.3575936964975,
4.74826029026393));
#209014=CARTESIAN_POINT('Ctrl Pts',(-16.4610282875234,17.7983958982468,
4.87543609694536));
#209015=CARTESIAN_POINT('Ctrl Pts',(-18.6914600224833,16.535174687256,5.0026119036268));
#209016=CARTESIAN_POINT('Ctrl Pts',(-20.9609195464861,17.7268571202586,
5.12978771030823));
#209017=CARTESIAN_POINT('Ctrl Pts',(-21.1873186048029,20.280148529128,5.25696351698966));
#209018=CARTESIAN_POINT('Ctrl Pts',(-19.1629501133386,21.8525625213641,
5.38413932367111));
#209019=CARTESIAN_POINT('Ctrl Pts',(-16.7450465165327,21.0015068541093,
5.51131513035253));
#209020=CARTESIAN_POINT('Ctrl Pts',(-16.1518842924324,18.5077722795978,
5.63849093703398));
#209021=CARTESIAN_POINT('Ctrl Pts',(-17.9276529658501,16.6592054913206,
5.7656667437154));
#209022=CARTESIAN_POINT('Ctrl Pts',(-20.4431949955591,17.1517517825272,
5.89284255039684));
#209023=CARTESIAN_POINT('Ctrl Pts',(-21.390656701448,19.5335305019064,6.02001835707826));
#209024=CARTESIAN_POINT('Ctrl Pts',(-19.9008007744695,21.6194075042871,
6.14719416375971));
#209025=CARTESIAN_POINT('Ctrl Pts',(-17.3404775567387,21.4957201041125,
6.27436997044113));
#209026=CARTESIAN_POINT('Ctrl Pts',(-16.0586246889428,19.2759438141371,
6.40154577712258));
#209027=CARTESIAN_POINT('Ctrl Pts',(-17.2312626165228,16.9965856055586,
6.528721583804));
#209028=CARTESIAN_POINT('Ctrl Pts',(-19.7825688230421,16.7488151618222,
6.65589739048545));
#209029=CARTESIAN_POINT('Ctrl Pts',(-21.3718782159412,18.7599464866879,
6.78307319716687));
#209030=CARTESIAN_POINT('Ctrl Pts',(-20.5410980709011,21.1848914144791,
6.91024900384832));
#209031=CARTESIAN_POINT('Ctrl Pts',(-18.0524176069647,21.7989134830039,
7.03742481052974));
#209032=CARTESIAN_POINT('Ctrl Pts',(-16.189046684864,20.0386855548983,7.16460061721119));
#209033=CARTESIAN_POINT('Ctrl Pts',(-16.6605124717835,17.5191075021328,
7.2917764238926));
#209034=CARTESIAN_POINT('Ctrl Pts',(-19.0342743706913,16.551735805469,7.41895223057406));
#209035=CARTESIAN_POINT('Ctrl Pts',(-21.1325531716193,18.024073954737,7.54612803725548));
#209036=CARTESIAN_POINT('Ctrl Pts',(-21.0303083085858,20.5853430815951,
7.67330384393691));
#209037=CARTESIAN_POINT('Ctrl Pts',(-18.8213430973923,21.8857377324416,
7.80047965061835));
#209038=CARTESIAN_POINT('Ctrl Pts',(-16.5322460154652,20.7322265267193,
7.92765545729978));
#209039=CARTESIAN_POINT('Ctrl Pts',(-16.2631215580847,18.1830844006987,
8.05483126398122));
#209040=CARTESIAN_POINT('Ctrl Pts',(-18.2608747111494,16.5769910373997,
8.18200707066265));
#209041=CARTESIAN_POINT('Ctrl Pts',(-20.6926909512673,17.3874374122526,
8.30918287734408));
#209042=CARTESIAN_POINT('Ctrl Pts',(-21.3275298136684,19.8708892783048,
8.43635868402552));
#209043=CARTESIAN_POINT('Ctrl Pts',(-19.5829660446433,21.7489336888602,
8.56353449070696));
#209044=CARTESIAN_POINT('Ctrl Pts',(-17.0595286224332,21.2985814618163,
8.69071029738838));
#209045=CARTESIAN_POINT('Ctrl Pts',(-16.0723147597259,18.9330028134741,
8.81788610406983));
#209046=CARTESIAN_POINT('Ctrl Pts',(-17.5270319021526,16.8224693293182,
8.94506191075126));
#209047=CARTESIAN_POINT('Ctrl Pts',(-20.0890673614655,16.90326448658,9.07223771743269));
#209048=CARTESIAN_POINT('Ctrl Pts',(-21.4079126215994,19.1012637431849,
9.19941352411413));
#209049=CARTESIAN_POINT('Ctrl Pts',(-20.2736090131502,21.3999392044174,
9.32658933079555));
#209050=CARTESIAN_POINT('Ctrl Pts',(-17.726809694048,21.6903988064862,9.453765137477));
#209051=CARTESIAN_POINT('Ctrl Pts',(-16.1040449673761,19.7061638924493,
9.58094094415843));
#209052=CARTESIAN_POINT('Ctrl Pts',(-16.894100749718,17.2676468404274,9.70811675083986));
#209053=CARTESIAN_POINT('Ctrl Pts',(-19.3721498971671,16.6120356942131,
9.83529255752129));
#209054=CARTESIAN_POINT('Ctrl Pts',(-21.2647361220149,18.3408129886411,
9.96246836420274));
#209055=CARTESIAN_POINT('Ctrl Pts',(-20.8355290301125,20.8679328560937,
10.0896441708842));
#209056=CARTESIAN_POINT('Ctrl Pts',(-18.4782994886839,21.8749196689318,
10.2168199775656));
#209057=CARTESIAN_POINT('Ctrl Pts',(-16.3556592958241,20.4379255270265,
10.3439957842471));
#209058=CARTESIAN_POINT('Ctrl Pts',(-16.4149990825736,17.875303365661,10.4711715909285));
#209059=CARTESIAN_POINT('Ctrl Pts',(-18.6018782776321,16.5380999636187,
10.59834739761));
#209060=CARTESIAN_POINT('Ctrl Pts',(-20.9099709525642,17.65311644607,10.7255232042914));
#209061=CARTESIAN_POINT('Ctrl Pts',(-21.2217453345073,20.1973943960938,
10.8526990109728));
#209062=CARTESIAN_POINT('Ctrl Pts',(-19.2511677789294,21.8367167102424,
10.9798748176543));
#209063=CARTESIAN_POINT('Ctrl Pts',(-16.806120885236,21.0671069131022,11.1070506243357));
#209064=CARTESIAN_POINT('Ctrl Pts',(-16.1297834216659,18.5946342261783,
11.2342264310171));
#209065=CARTESIAN_POINT('Ctrl Pts',(-17.8426530328072,16.6876388807614,
11.3614022376985));
#209066=CARTESIAN_POINT('Ctrl Pts',(-20.3732781631159,17.0956707447917,
11.48857804438));
#209067=CARTESIAN_POINT('Ctrl Pts',(-21.3999673238431,19.4443859083351,
11.6157538510614));
#209068=CARTESIAN_POINT('Ctrl Pts',(-19.9807969335377,21.5789839865442,
11.7429296577429));
#209069=CARTESIAN_POINT('Ctrl Pts',(-17.4177677416566,21.5411037307608,
11.8701054644243));
#209070=CARTESIAN_POINT('Ctrl Pts',(-16.062299952218,19.3654979245523,11.9972812711057));
#209071=CARTESIAN_POINT('Ctrl Pts',(-17.157951132213,17.0481498617898,12.1244570777871));
#209072=CARTESIAN_POINT('Ctrl Pts',(-19.6995293277776,16.7150825592159,
12.2516328844686));
#209073=CARTESIAN_POINT('Ctrl Pts',(-21.3552942926149,18.671864594454,12.37880869115));
#209074=CARTESIAN_POINT('Ctrl Pts',(-20.6061844398505,21.1232699017635,
12.5059844978315));
#209075=CARTESIAN_POINT('Ctrl Pts',(-18.1394615643946,21.8202862630607,
12.6331603045129));
#209076=CARTESIAN_POINT('Ctrl Pts',(-16.2181908023896,20.1234444285697,
12.7603361111943));
#209077=CARTESIAN_POINT('Ctrl Pts',(-16.605018830463,17.5894914635544,12.8875119178758));
#209078=CARTESIAN_POINT('Ctrl Pts',(-18.9450549421127,16.5431719385577,
13.0146877245572));
#209079=CARTESIAN_POINT('Ctrl Pts',(-21.091461243921,17.9444190758505,13.1418635312386));
#209080=CARTESIAN_POINT('Ctrl Pts',(-21.0750431749784,20.5076755981723,
13.2690393379201));
#209081=CARTESIAN_POINT('Ctrl Pts',(-18.9108632945195,21.8813127399352,
13.3962151446015));
#209082=CARTESIAN_POINT('Ctrl Pts',(-16.584422318713,20.8051036811079,13.5233909512829));
#209083=CARTESIAN_POINT('Ctrl Pts',(-16.2300854476496,18.2664034360971,
13.6505667579644));
#209084=CARTESIAN_POINT('Ctrl Pts',(-18.1729347679036,16.5943119101923,
13.7777425646458));
#209085=CARTESIAN_POINT('Ctrl Pts',(-20.6305266149702,17.3228692967068,
13.9049183713272));
#209086=CARTESIAN_POINT('Ctrl Pts',(-21.3481730045189,19.7836694128848,
14.0320941780087));
#209087=CARTESIAN_POINT('Ctrl Pts',(-19.6674779162968,21.7190808866133,
14.1592699846901));
#209088=CARTESIAN_POINT('Ctrl Pts',(-17.1303747780463,21.3534838159302,
14.2864457913715));
#209089=CARTESIAN_POINT('Ctrl Pts',(-16.0644982487317,19.0222908216738,
14.413621598053));
#209090=CARTESIAN_POINT('Ctrl Pts',(-17.447723888241,16.8642267859192,14.5407974047344));
#209091=CARTESIAN_POINT('Ctrl Pts',(-20.0110280249899,16.859181516911,14.6679732114158));
#209092=CARTESIAN_POINT('Ctrl Pts',(-21.4027382101088,19.0117837358195,
14.7951490180973));
#209093=CARTESIAN_POINT('Ctrl Pts',(-20.3460467280269,21.3471545123578,
14.9223248247787));
#209094=CARTESIAN_POINT('Ctrl Pts',(-17.8104024278843,21.7227361085096,
15.0495006314601));
#209095=CARTESIAN_POINT('Ctrl Pts',(-16.1221015752275,19.7939557210286,
15.1766764381416));
#209096=CARTESIAN_POINT('Ctrl Pts',(-16.8300554146003,17.3303496418165,
15.303852244823));
#209097=CARTESIAN_POINT('Ctrl Pts',(-19.284760238949,16.5921235399122,15.4310280515045));
#209098=CARTESIAN_POINT('Ctrl Pts',(-21.2341767280976,18.2565540443337,
15.5582038581859));
#209099=CARTESIAN_POINT('Ctrl Pts',(-20.8898362476853,20.7966294734819,
15.6853796648673));
#209100=CARTESIAN_POINT('Ctrl Pts',(-18.5676498163098,21.8819882759749,
15.8125554715487));
#209101=CARTESIAN_POINT('Ctrl Pts',(-16.3980793536131,20.5168811154897,
15.9397312782302));
#209102=CARTESIAN_POINT('Ctrl Pts',(-16.3715711003901,17.9537090836658,
16.0669070849116));
#209103=CARTESIAN_POINT('Ctrl Pts',(-18.5124447336848,16.5440234313033,
16.1940828915931));
#209104=CARTESIAN_POINT('Ctrl Pts',(-20.8565815725531,17.5811232494858,
16.3212586982745));
#209105=CARTESIAN_POINT('Ctrl Pts',(-21.253381560874,20.1135338247049,16.4484345049559));
#209106=CARTESIAN_POINT('Ctrl Pts',(-19.338805337548,21.8179256333241,16.5756103116374));
#209107=CARTESIAN_POINT('Ctrl Pts',(-16.8693577554744,21.1306249774212,
16.7027861183188));
#209108=CARTESIAN_POINT('Ctrl Pts',(-16.1106037000031,18.6821875500976,
16.8299619250002));
#209109=CARTESIAN_POINT('Ctrl Pts',(-17.7586529234411,16.7189027237572,
16.9571377316817));
#209110=CARTESIAN_POINT('Ctrl Pts',(-20.3015225527551,17.0419624713682,
17.0843135383631));
#209111=CARTESIAN_POINT('Ctrl Pts',(-21.4062875313382,19.354979525847,17.2114893450445));
#209112=CARTESIAN_POINT('Ctrl Pts',(-20.0593945607884,21.5359043017382,
17.338665151726));
#209113=CARTESIAN_POINT('Ctrl Pts',(-17.4965343439791,21.5838736806199,
17.4658409584074));
#209114=CARTESIAN_POINT('Ctrl Pts',(-16.0689720607886,19.4548787346826,
17.5930167650888));
#209115=CARTESIAN_POINT('Ctrl Pts',(-17.0864075015351,17.1021401864965,
17.7201925717703));
#209116=CARTESIAN_POINT('Ctrl Pts',(-19.6154067985012,16.6841496265959,
17.8473683784517));
#209117=CARTESIAN_POINT('Ctrl Pts',(-21.3357700641153,18.584387450276,17.9745441851331));
#209118=CARTESIAN_POINT('Ctrl Pts',(-20.6691707799709,21.0595033963588,
18.1017199918146));
#209119=CARTESIAN_POINT('Ctrl Pts',(-18.2271724154379,21.8387322073577,
18.228895798496));
#209120=CARTESIAN_POINT('Ctrl Pts',(-16.2501569024917,20.207179813531,18.3560716051774));
#209121=CARTESIAN_POINT('Ctrl Pts',(-16.5519132667841,17.6616942707386,
18.4832474118589));
#209122=CARTESIAN_POINT('Ctrl Pts',(-18.8555987732945,16.537600573676,18.6104232185403));
#209123=CARTESIAN_POINT('Ctrl Pts',(-21.0477249524445,17.8661849205939,
18.7375990252217));
#209124=CARTESIAN_POINT('Ctrl Pts',(-21.1171520939507,20.4285536338248,
18.8647748319032));
#209125=CARTESIAN_POINT('Ctrl Pts',(-19.0001851038609,21.8738924587027,
18.9919506385846));
#209126=CARTESIAN_POINT('Ctrl Pts',(-16.639009803247,20.8761927289634,19.119126445266));
#209127=CARTESIAN_POINT('Ctrl Pts',(-16.1998579765528,18.3507820268139,
19.2463022519475));
#209128=CARTESIAN_POINT('Ctrl Pts',(-18.0856241733337,16.6145679183314,
19.3734780586289));
#209129=CARTESIAN_POINT('Ctrl Pts',(-20.5662349414884,17.2604191027876,
19.5006538653103));
#209130=CARTESIAN_POINT('Ctrl Pts',(-21.3658838853536,19.695807173002,19.6278296719918));
#209131=CARTESIAN_POINT('Ctrl Pts',(-19.7509426921062,21.6864147924606,
19.7550054786732));
#209132=CARTESIAN_POINT('Ctrl Pts',(-17.2030197464517,21.4059829044279,
19.8821812853547));
#209133=CARTESIAN_POINT('Ctrl Pts',(-16.059676065617,19.1117905859247,20.0093570920361));
#209134=CARTESIAN_POINT('Ctrl Pts',(-17.3698587893405,16.908616461354,20.1365328987175));
#209135=CARTESIAN_POINT('Ctrl Pts',(-19.9315560549264,16.8177368822917,
20.2637087053989));
#209136=CARTESIAN_POINT('Ctrl Pts',(-21.3945706447594,18.9225266095884,
20.3908845120804));
#209137=CARTESIAN_POINT('Ctrl Pts',(-20.4166754991338,21.2919748133934,
20.5180603187618));
#209138=CARTESIAN_POINT('Ctrl Pts',(-17.8950325316693,21.7522538440923,
20.6452361254433));
#209139=CARTESIAN_POINT('Ctrl Pts',(-16.1430853073993,19.881097796524,20.7724119321247));
#209140=CARTESIAN_POINT('Ctrl Pts',(-16.7681508238931,17.395153974591,20.8995877388061));
#209141=CARTESIAN_POINT('Ctrl Pts',(-19.1967429841419,16.5751643826307,
21.0267635454876));
#209142=CARTESIAN_POINT('Ctrl Pts',(-21.2008317885977,18.1733360181572,
21.153939352169));
#209143=CARTESIAN_POINT('Ctrl Pts',(-20.9416888395956,20.7236046919281,
21.2811151588505));
#209144=CARTESIAN_POINT('Ctrl Pts',(-18.6572569308498,21.8859506052002,
21.4082909655318));
#209145=CARTESIAN_POINT('Ctrl Pts',(-16.4429843423898,20.5945843440041,
21.5354667722133));
#209146=CARTESIAN_POINT('Ctrl Pts',(-16.3310538134642,18.033115434702,21.6626425788947));
#209147=CARTESIAN_POINT('Ctrl Pts',(-18.4227563631869,16.5537305545665,
21.7898183855762));
#209148=CARTESIAN_POINT('Ctrl Pts',(-20.8017893666684,17.50940661932,21.9169941922576));
#209149=CARTESIAN_POINT('Ctrl Pts',(-21.2802300646426,20.0318897120323,
22.0441699989391));
#209150=CARTESIAN_POINT('Ctrl Pts',(-20.0469416504615,21.2025211683863,
22.12895387006));
#209151=CARTESIAN_POINT('Ctrl Pts',(-19.3190223666151,21.3973017229923,
22.1713458056205));
#209152=CARTESIAN_POINT('Ctrl Pts',(-16.8880690316762,20.7654464739225,
-0.171094734500184));
#209153=CARTESIAN_POINT('Ctrl Pts',(-16.3702699845374,20.1505948657621,
-0.128684141441329));
#209154=CARTESIAN_POINT('Ctrl Pts',(-16.006827020915,18.3736777454539,-0.0438816128219947));
#209155=CARTESIAN_POINT('Ctrl Pts',(-17.9658924760107,16.4608289063181,
0.0833128513578173));
#209156=CARTESIAN_POINT('Ctrl Pts',(-20.6289599190898,17.0785068518555,
0.210488658039252));
#209157=CARTESIAN_POINT('Ctrl Pts',(-21.5536817767679,19.6490616868026,
0.337664464720685));
#209158=CARTESIAN_POINT('Ctrl Pts',(-19.8914411384235,21.8195502173065,
0.46484027140212));
#209159=CARTESIAN_POINT('Ctrl Pts',(-17.1673608230486,21.5959088255693,
0.592016078083554));
#209160=CARTESIAN_POINT('Ctrl Pts',(-15.8805536346544,19.1847528689885,
0.719191884764988));
#209161=CARTESIAN_POINT('Ctrl Pts',(-17.2116173157294,16.7974221125058,
0.846367691446423));
#209162=CARTESIAN_POINT('Ctrl Pts',(-19.9393669463845,16.6245315463164,
0.973543498127856));
#209163=CARTESIAN_POINT('Ctrl Pts',(-21.5612701613726,18.8244966062191,
1.10071930480929));
#209164=CARTESIAN_POINT('Ctrl Pts',(-20.5893269556668,21.3790901636359,
1.22789511149073));
#209165=CARTESIAN_POINT('Ctrl Pts',(-17.9152372155514,21.9445770767739,
1.35507091817216));
#209166=CARTESIAN_POINT('Ctrl Pts',(-15.9923111005858,20.0021862799634,
1.4822467248536));
#209167=CARTESIAN_POINT('Ctrl Pts',(-16.5847145959355,17.3339261996511,
1.60942253153503));
#209168=CARTESIAN_POINT('Ctrl Pts',(-19.1489539390206,16.3877674101879,
1.73659833821646));
#209169=CARTESIAN_POINT('Ctrl Pts',(-21.332498855497,18.0317479516957,1.8637741448979));
#209170=CARTESIAN_POINT('Ctrl Pts',(-21.1320823232458,20.7576197505752,
1.99094995157933));
#209171=CARTESIAN_POINT('Ctrl Pts',(-18.7315741166753,22.064563561331,2.11812575826077));
#209172=CARTESIAN_POINT('Ctrl Pts',(-16.3332914994529,20.7535401040407,
2.2453015649422));
#209173=CARTESIAN_POINT('Ctrl Pts',(-16.1375099308779,18.0273317449088,
2.37247737162363));
#209174=CARTESIAN_POINT('Ctrl Pts',(-18.3238468422098,16.387065593537,2.49965317830507));
#209175=CARTESIAN_POINT('Ctrl Pts',(-20.8864738199611,17.3375839607775,
2.62682898498651));
#209176=CARTESIAN_POINT('Ctrl Pts',(-21.4743396649076,20.006845280278,2.75400479166794));
#209177=CARTESIAN_POINT('Ctrl Pts',(-19.5481139522653,21.9459679438018,
2.88118059834937));
#209178=CARTESIAN_POINT('Ctrl Pts',(-16.8749892178732,21.3759272738012,
3.00835640503081));
#209179=CARTESIAN_POINT('Ctrl Pts',(-15.9073914929419,18.8197001987301,
3.13553221171224));
#209180=CARTESIAN_POINT('Ctrl Pts',(-17.5330316340844,16.6224664055047,
3.26270801839368));
#209181=CARTESIAN_POINT('Ctrl Pts',(-20.2604857104729,16.8000515222033,
3.38988382507511));
#209182=CARTESIAN_POINT('Ctrl Pts',(-21.5874838918795,19.1895322272068,
3.51705963175655));
#209183=CARTESIAN_POINT('Ctrl Pts',(-20.2965877096769,21.5987082811702,
3.64423543843798));
#209184=CARTESIAN_POINT('Ctrl Pts',(-17.5721142889738,21.8173101851209,
3.77141124511941));
#209185=CARTESIAN_POINT('Ctrl Pts',(-15.9135988933785,19.64478426004,3.89858705180085));
#209186=CARTESIAN_POINT('Ctrl Pts',(-16.8426264592725,17.0742882000792,
4.02576285848228));
#209187=CARTESIAN_POINT('Ctrl Pts',(-19.5068718569032,16.4640925972449,
4.15293866516372));
#209188=CARTESIAN_POINT('Ctrl Pts',(-21.4620552956622,18.3740140441421,
4.28011447184515));
#209189=CARTESIAN_POINT('Ctrl Pts',(-20.914417322859,21.0518181563291,4.40729027852659));
#209190=CARTESIAN_POINT('Ctrl Pts',(-18.3663817882941,22.0407858641459,
4.53446608520802));
#209191=CARTESIAN_POINT('Ctrl Pts',(-16.15561314601,20.4336006779268,4.66164189188945));
#209192=CARTESIAN_POINT('Ctrl Pts',(-16.3103544095251,17.7047552528665,
4.78881769857089));
#209193=CARTESIAN_POINT('Ctrl Pts',(-18.6886400738904,16.3577958952085,
4.91599350525232));
#209194=CARTESIAN_POINT('Ctrl Pts',(-21.1085406551067,17.628474213878,5.04316931193375));
#209195=CARTESIAN_POINT('Ctrl Pts',(-21.3499475658771,20.3510217186868,
5.1703451186152));
#209196=CARTESIAN_POINT('Ctrl Pts',(-19.1913849489723,22.0276700543283,
5.29752092529662));
#209197=CARTESIAN_POINT('Ctrl Pts',(-16.613200029897,21.1201984373834,5.42469673197806));
#209198=CARTESIAN_POINT('Ctrl Pts',(-15.9807174516997,18.4611557523585,
5.5518725386595));
#209199=CARTESIAN_POINT('Ctrl Pts',(-17.8742007235803,16.4900486239617,
5.67904834534092));
#209200=CARTESIAN_POINT('Ctrl Pts',(-20.5564964664144,17.0152455017915,
5.80622415202237));
#209201=CARTESIAN_POINT('Ctrl Pts',(-21.5667648182011,19.5549108478334,
5.93339995870379));
#209202=CARTESIAN_POINT('Ctrl Pts',(-19.9781472705018,21.7790593365027,
6.06057576538524));
#209203=CARTESIAN_POINT('Ctrl Pts',(-17.2481018226055,21.6471727756692,
6.18775157206665));
#209204=CARTESIAN_POINT('Ctrl Pts',(-15.8812757272267,19.2802488990946,
6.31492737874811));
#209205=CARTESIAN_POINT('Ctrl Pts',(-17.1316470920802,16.849793455672,6.44210318542952));
#209206=CARTESIAN_POINT('Ctrl Pts',(-19.8520777967125,16.5855984636642,
6.56927899211098));
#209207=CARTESIAN_POINT('Ctrl Pts',(-21.5467415185955,18.7300464304477,
6.6964547987924));
#209208=CARTESIAN_POINT('Ctrl Pts',(-20.6608894755945,21.3157394459503,
6.82363060547384));
#209209=CARTESIAN_POINT('Ctrl Pts',(-18.0072359349844,21.9704646546564,
6.95080641215527));
#209210=CARTESIAN_POINT('Ctrl Pts',(-16.020343315961,20.0935523144076,7.07798221883671));
#209211=CARTESIAN_POINT('Ctrl Pts',(-16.5230622760143,17.4069530030642,
7.20515802551813));
#209212=CARTESIAN_POINT('Ctrl Pts',(-19.0541793715532,16.3754548396247,
7.33233383219958));
#209213=CARTESIAN_POINT('Ctrl Pts',(-21.291551766265,17.9453933670485,7.459509638881));
#209214=CARTESIAN_POINT('Ctrl Pts',(-21.1825291549937,20.6764474277986,
7.58668544556244));
#209215=CARTESIAN_POINT('Ctrl Pts',(-18.8271330168744,22.0630444294688,
7.71386125224388));
#209216=CARTESIAN_POINT('Ctrl Pts',(-16.3862931162597,20.8330676849425,
7.84103705892531));
#209217=CARTESIAN_POINT('Ctrl Pts',(-16.099328566354,18.1149445163563,7.96821286560675));
#209218=CARTESIAN_POINT('Ctrl Pts',(-18.2295115306668,16.4023842251376,
8.09538867228817));
#209219=CARTESIAN_POINT('Ctrl Pts',(-20.8225313535071,17.2665545850003,
8.22256447896962));
#209220=CARTESIAN_POINT('Ctrl Pts',(-21.4994532883798,19.9146329272319,
8.34974028565105));
#209221=CARTESIAN_POINT('Ctrl Pts',(-19.6392434745528,21.917171731113,8.47691609233248));
#209222=CARTESIAN_POINT('Ctrl Pts',(-16.9485289585702,21.4369659356584,
8.60409189901392));
#209223=CARTESIAN_POINT('Ctrl Pts',(-15.8958733042685,18.9145745532646,
8.73126770569535));
#209224=CARTESIAN_POINT('Ctrl Pts',(-17.4470227392911,16.6641351200123,
8.85844351237678));
#209225=CARTESIAN_POINT('Ctrl Pts',(-20.1788939321968,16.7502861378866,
8.98561931905823));
#209226=CARTESIAN_POINT('Ctrl Pts',(-21.5851646225432,19.093989395123,9.11279512573965));
#209227=CARTESIAN_POINT('Ctrl Pts',(-20.3756687349404,21.5450426198368,
9.23997093242109));
#209228=CARTESIAN_POINT('Ctrl Pts',(-17.6600436764829,21.8547566078734,
9.36714673910252));
#209229=CARTESIAN_POINT('Ctrl Pts',(-15.9297068876053,19.738987998227,9.49432254578396));
#209230=CARTESIAN_POINT('Ctrl Pts',(-16.7721349752896,17.1388231708385,
9.62149835246539));
#209231=CARTESIAN_POINT('Ctrl Pts',(-19.4144524560694,16.4397519704066,
9.74867415914682));
#209232=CARTESIAN_POINT('Ctrl Pts',(-21.432497042048,18.2831288340757,9.87584996582827));
#209233=CARTESIAN_POINT('Ctrl Pts',(-20.974838079563,20.9777699023008,10.0030257725097));
#209234=CARTESIAN_POINT('Ctrl Pts',(-18.4613492611758,22.0515092432722,
10.1302015791911));
#209235=CARTESIAN_POINT('Ctrl Pts',(-16.1980005730462,20.5192576554282,
10.2573773858725));
#209236=CARTESIAN_POINT('Ctrl Pts',(-16.2612739572708,17.7867608683564,
10.384553192554));
#209237=CARTESIAN_POINT('Ctrl Pts',(-18.5931200110123,16.3609150863178,
10.5117289992354));
#209238=CARTESIAN_POINT('Ctrl Pts',(-21.0542147106519,17.5498453163626,
10.6389048059168));
#209239=CARTESIAN_POINT('Ctrl Pts',(-21.3866564220343,20.2627818657572,
10.7660806125983));
#209240=CARTESIAN_POINT('Ctrl Pts',(-19.2854505086261,22.0107738342645,
10.8932564192797));
#209241=CARTESIAN_POINT('Ctrl Pts',(-16.6783229804319,21.1901470833962,
11.0204322259611));
#209242=CARTESIAN_POINT('Ctrl Pts',(-15.9571515279862,18.5537757232337,
11.1476080326426));
#209243=CARTESIAN_POINT('Ctrl Pts',(-17.7835661979594,16.5203668450652,
11.274783839324));
#209244=CARTESIAN_POINT('Ctrl Pts',(-20.4819448907301,16.9554468870216,
11.4019596460055));
#209245=CARTESIAN_POINT('Ctrl Pts',(-21.5766926359512,19.4598569147211,
11.5291354526869));
#209246=CARTESIAN_POINT('Ctrl Pts',(-20.0634463250904,21.735956168966,11.6563112593683));
#209247=CARTESIAN_POINT('Ctrl Pts',(-17.330515525704,21.6955648546388,11.7834870660497));
#209248=CARTESIAN_POINT('Ctrl Pts',(-15.8851946214135,19.3757394956669,
11.9106628727312));
#209249=CARTESIAN_POINT('Ctrl Pts',(-17.053475835173,16.9047758743069,12.0378386794126));
#209250=CARTESIAN_POINT('Ctrl Pts',(-19.7635336650682,16.5496297478578,
12.165014486094));
#209251=CARTESIAN_POINT('Ctrl Pts',(-21.5290582573291,18.6361256444822,
12.2921902927755));
#209252=CARTESIAN_POINT('Ctrl Pts',(-20.7302903793709,21.2500330815674,
12.4193660994569));
#209253=CARTESIAN_POINT('Ctrl Pts',(-18.1000499820946,21.9932542229807,
12.5465419061383));
#209254=CARTESIAN_POINT('Ctrl Pts',(-16.0514193788707,20.1839298009815,
12.6737177128198));
#209255=CARTESIAN_POINT('Ctrl Pts',(-16.4638899958019,17.4820026734157,
12.8008935195012));
#209256=CARTESIAN_POINT('Ctrl Pts',(-18.9590456426674,16.3663232793141,
12.9280693261827));
#209257=CARTESIAN_POINT('Ctrl Pts',(-21.2477358802935,17.8604582158923,
13.0552451328641));
#209258=CARTESIAN_POINT('Ctrl Pts',(-21.2302294677946,20.5936314153126,
13.1824209395455));
#209259=CARTESIAN_POINT('Ctrl Pts',(-18.9225874520683,22.0583261069674,
13.309596746227));
#209260=CARTESIAN_POINT('Ctrl Pts',(-16.4419281541264,20.9107758204687,
13.4367725529084));
#209261=CARTESIAN_POINT('Ctrl Pts',(-16.0641025127507,18.2037867186756,
13.5639483595899));
#209262=CARTESIAN_POINT('Ctrl Pts',(-18.1357421033992,16.4208532877909,
13.6911241662712));
#209263=CARTESIAN_POINT('Ctrl Pts',(-20.756246182106,17.1977062893226,13.8182999729527));
#209264=CARTESIAN_POINT('Ctrl Pts',(-21.5214649034841,19.8216313113002,
13.9454757796341));
#209265=CARTESIAN_POINT('Ctrl Pts',(-19.7293575854992,21.8853400052135,
14.0726515863156));
#209266=CARTESIAN_POINT('Ctrl Pts',(-17.0240714616778,21.495507732604,14.199827392997));
#209267=CARTESIAN_POINT('Ctrl Pts',(-15.8875386416327,19.0097814078715,
14.3270031996784));
#209268=CARTESIAN_POINT('Ctrl Pts',(-17.3624574465728,16.7086606523826,
14.4541790063599));
#209269=CARTESIAN_POINT('Ctrl Pts',(-20.0956814167509,16.7032809356367,
14.5813548130413));
#209270=CARTESIAN_POINT('Ctrl Pts',(-21.5796472025402,18.9985778138453,
14.7085306197227));
#209271=CARTESIAN_POINT('Ctrl Pts',(-20.4529083007835,21.4887588634431,
14.8357064264042));
#209272=CARTESIAN_POINT('Ctrl Pts',(-17.749177720539,21.8892375294908,14.9628822330856));
#209273=CARTESIAN_POINT('Ctrl Pts',(-15.9489604567358,19.8325994923992,
15.090058039767));
#209274=CARTESIAN_POINT('Ctrl Pts',(-16.7038441148284,17.2056825018467,
15.2172338464485));
#209275=CARTESIAN_POINT('Ctrl Pts',(-19.321269791881,16.4185198518091,15.3444096531299));
#209276=CARTESIAN_POINT('Ctrl Pts',(-21.3999118849568,18.1932844168717,
15.4715854598113));
#209277=CARTESIAN_POINT('Ctrl Pts',(-21.0327452887372,20.9017398629015,
15.5987612664928));
#209278=CARTESIAN_POINT('Ctrl Pts',(-18.5566225663247,22.05904642387,15.7259370731742));
#209279=CARTESIAN_POINT('Ctrl Pts',(-16.2432326300242,20.6034471606347,
15.8531128798556));
#209280=CARTESIAN_POINT('Ctrl Pts',(-16.2149671612184,17.8703640525348,
15.9802886865371));
#209281=CARTESIAN_POINT('Ctrl Pts',(-18.4977579731839,16.367231216983,16.1074644932185));
#209282=CARTESIAN_POINT('Ctrl Pts',(-20.9972861819192,17.4730797356526,
16.2346402999));
#209283=CARTESIAN_POINT('Ctrl Pts',(-21.4203897941269,20.1733622293642,
16.3618161065814));
#209284=CARTESIAN_POINT('Ctrl Pts',(-19.378897506378,21.9907371085704,16.4889919132628));
#209285=CARTESIAN_POINT('Ctrl Pts',(-16.7457517833806,21.2578757206061,
16.6161677199442));
#209286=CARTESIAN_POINT('Ctrl Pts',(-15.9367003945299,18.6471329024206,
16.7433435266257));
#209287=CARTESIAN_POINT('Ctrl Pts',(-17.6939977737036,16.5537031487253,
16.8705193333071));
#209288=CARTESIAN_POINT('Ctrl Pts',(-20.4054326456862,16.8981783256312,
16.9976951399886));
#209289=CARTESIAN_POINT('Ctrl Pts',(-21.5834318060615,19.364523838868,17.12487094667));
#209290=CARTESIAN_POINT('Ctrl Pts',(-20.1472541400588,21.6900207587073,
17.2520467533514));
#209291=CARTESIAN_POINT('Ctrl Pts',(-17.4145035169965,21.7411699978141,
17.3792225600329));
#209292=CARTESIAN_POINT('Ctrl Pts',(-15.8923090199021,19.4710453039866,
17.5063983667143));
#209293=CARTESIAN_POINT('Ctrl Pts',(-16.9771896218132,16.9623451839844,
17.6335741733957));
#209294=CARTESIAN_POINT('Ctrl Pts',(-19.6738347057625,16.5166462904161,
17.7607499800772));
#209295=CARTESIAN_POINT('Ctrl Pts',(-21.5082397798925,18.542849694944,17.8879257867586));
#209296=CARTESIAN_POINT('Ctrl Pts',(-20.7974520447164,21.1820395342675,
18.01510159344));
#209297=CARTESIAN_POINT('Ctrl Pts',(-18.1935751307804,22.0129229374272,
18.1422774001214));
#209298=CARTESIAN_POINT('Ctrl Pts',(-16.085504491823,20.2732159524167,18.2694532068029));
#209299=CARTESIAN_POINT('Ctrl Pts',(-16.4072640974092,17.5589917596816,
18.3966290134843));
#209300=CARTESIAN_POINT('Ctrl Pts',(-18.8636594801795,16.3603825921271,
18.5238048201658));
#209301=CARTESIAN_POINT('Ctrl Pts',(-21.2011003373174,17.7770379672497,
18.6509806268472));
#209302=CARTESIAN_POINT('Ctrl Pts',(-21.2751297607576,20.5092645052679,
18.7781564335287));
#209303=CARTESIAN_POINT('Ctrl Pts',(-19.0178303484736,22.0504139399173,
18.90533224021));
#209304=CARTESIAN_POINT('Ctrl Pts',(-16.5001342089838,20.9865773169943,
19.0325080468915));
#209305=CARTESIAN_POINT('Ctrl Pts',(-16.0318712814367,18.2937587135751,
19.1596838535729));
#209306=CARTESIAN_POINT('Ctrl Pts',(-18.042643743939,16.4424520540833,19.2868596602544));
#209307=CARTESIAN_POINT('Ctrl Pts',(-20.6876926536642,17.1311163109758,
19.4140354669358));
#209308=CARTESIAN_POINT('Ctrl Pts',(-21.5403498275698,19.7279447383034,
19.5412112736172));
#209309=CARTESIAN_POINT('Ctrl Pts',(-19.8183551892704,21.8505084960413,
19.6683870802987));
#209310=CARTESIAN_POINT('Ctrl Pts',(-17.1015320197568,21.5514869529538,
19.7955628869801));
#209311=CARTESIAN_POINT('Ctrl Pts',(-15.8823967990051,19.1052140557062,
19.9227386936616));
#209312=CARTESIAN_POINT('Ctrl Pts',(-17.2794307188022,16.7559928917323,
20.049914500343));
#209313=CARTESIAN_POINT('Ctrl Pts',(-20.0109412993294,16.6590889620223,
20.1770903070244));
#209314=CARTESIAN_POINT('Ctrl Pts',(-21.5709382143749,18.9034038883535,
20.3042661137059));
#209315=CARTESIAN_POINT('Ctrl Pts',(-20.5282190091016,21.4299213366298,
20.4314419203873));
#209316=CARTESIAN_POINT('Ctrl Pts',(-17.839417901151,21.920711977366,20.5586177270687));
#209317=CARTESIAN_POINT('Ctrl Pts',(-15.9713351874333,19.9255181617605,
20.6857935337502));
#209318=CARTESIAN_POINT('Ctrl Pts',(-16.6378359073908,17.2747826734461,
20.8129693404316));
#209319=CARTESIAN_POINT('Ctrl Pts',(-19.227417928117,16.4004364825627,20.940145147113));
#209320=CARTESIAN_POINT('Ctrl Pts',(-21.3643565302024,18.1045499196127,
21.0673209537945));
#209321=CARTESIAN_POINT('Ctrl Pts',(-21.0880351566437,20.8238743140973,
21.1944967604759));
#209322=CARTESIAN_POINT('Ctrl Pts',(-18.6521696806324,22.0632714134299,
21.3216725671574));
#209323=CARTESIAN_POINT('Ctrl Pts',(-16.2911143425161,20.6863012877323,
21.4488483738387));
#209324=CARTESIAN_POINT('Ctrl Pts',(-16.1717640085979,17.9550342010845,
21.5760241805202));
#209325=CARTESIAN_POINT('Ctrl Pts',(-18.4021242165115,16.3775818193965,
21.7031999872016));
#209326=CARTESIAN_POINT('Ctrl Pts',(-20.9388618348603,17.3966090547766,
21.8303757938831));
#209327=CARTESIAN_POINT('Ctrl Pts',(-21.4490180684747,20.086305979354,21.9575516005645));
#209328=CARTESIAN_POINT('Ctrl Pts',(-20.1339757340687,21.3345378652548,
22.0423354716855));
#209329=CARTESIAN_POINT('Ctrl Pts',(-19.3578031346334,21.5422303014122,
22.0847274072459));
#209330=CARTESIAN_POINT('Ctrl Pts',(-16.7733106781414,20.8620837377565,
-0.257713132874658));
#209331=CARTESIAN_POINT('Ctrl Pts',(-16.2233209547904,20.2090078625832,
-0.215302539815803));
#209332=CARTESIAN_POINT('Ctrl Pts',(-15.8372833671953,18.3216228609763,
-0.130500011196469));
#209333=CARTESIAN_POINT('Ctrl Pts',(-17.9181405522913,16.2898554993676,
-0.00330554701665755));
#209334=CARTESIAN_POINT('Ctrl Pts',(-20.7467663181702,16.9459334204518,
0.123870259664777));
#209335=CARTESIAN_POINT('Ctrl Pts',(-21.7289765433362,19.6762952284609,
0.251046066346211));
#209336=CARTESIAN_POINT('Ctrl Pts',(-19.9633972633481,21.9817192979426,
0.378221873027645));
#209337=CARTESIAN_POINT('Ctrl Pts',(-17.0699655598372,21.7441745055157,
0.50539767970908));
#209338=CARTESIAN_POINT('Ctrl Pts',(-15.703159781685,19.1831211299953,0.632573486390514));
#209339=CARTESIAN_POINT('Ctrl Pts',(-17.1169734025524,16.6473741262867,
0.759749293071947));
#209340=CARTESIAN_POINT('Ctrl Pts',(-20.0143025363638,16.4637352509469,
0.886925099753383));
#209341=CARTESIAN_POINT('Ctrl Pts',(-21.7370366847608,18.8004683549644,
1.01410090643482));
#209342=CARTESIAN_POINT('Ctrl Pts',(-20.7046694415748,21.5138766002705,
1.14127671311625));
#209343=CARTESIAN_POINT('Ctrl Pts',(-17.8643361414099,22.1145188622328,
1.26845251979769));
#209344=CARTESIAN_POINT('Ctrl Pts',(-15.8218650170646,20.0513729702491,
1.39562832647912));
#209345=CARTESIAN_POINT('Ctrl Pts',(-16.4510972188617,17.217231749811,1.52280413316055));
#209346=CARTESIAN_POINT('Ctrl Pts',(-19.1747509117416,16.2122518956796,
1.64997993984199));
#209347=CARTESIAN_POINT('Ctrl Pts',(-21.4940430602564,17.9584358800158,
1.77715574652343));
#209348=CARTESIAN_POINT('Ctrl Pts',(-21.281166976886,20.8537704404796,1.90433155320486));
#209349=CARTESIAN_POINT('Ctrl Pts',(-18.7314233036813,22.2419647001733,
2.03150735988629));
#209350=CARTESIAN_POINT('Ctrl Pts',(-16.1840435808866,20.8494371693366,
2.15868316656773));
#209351=CARTESIAN_POINT('Ctrl Pts',(-15.9760906089126,17.9537451252482,
2.28585897324916));
#209352=CARTESIAN_POINT('Ctrl Pts',(-18.2983483258012,16.2115064482945,
2.4130347799306));
#209353=CARTESIAN_POINT('Ctrl Pts',(-21.0202894153674,17.2211169076559,
2.54021058661203));
#209354=CARTESIAN_POINT('Ctrl Pts',(-21.64470186884,20.0563216126004,2.66738639329346));
#209355=CARTESIAN_POINT('Ctrl Pts',(-19.5987260165054,22.1159961970718,
2.7945621999749));
#209356=CARTESIAN_POINT('Ctrl Pts',(-16.75941771481,21.5105170790144,2.92173800665633));
#209357=CARTESIAN_POINT('Ctrl Pts',(-15.7316661034645,18.7953737630709,
3.04891381333777));
#209358=CARTESIAN_POINT('Ctrl Pts',(-17.4583694962879,16.4615417238828,
3.1760896200192));
#209359=CARTESIAN_POINT('Ctrl Pts',(-20.3553847017321,16.6501670018626,
3.30326542670064));
#209360=CARTESIAN_POINT('Ctrl Pts',(-21.7648800778091,19.1881976126941,
3.43044123338207));
#209361=CARTESIAN_POINT('Ctrl Pts',(-20.3937311001358,21.7471479984566,
3.5576170400635));
#209362=CARTESIAN_POINT('Ctrl Pts',(-17.4998818526145,21.9793400068086,
3.68479284674494));
#209363=CARTESIAN_POINT('Ctrl Pts',(-15.7382594073102,19.671751881433,3.81196865342637));
#209364=CARTESIAN_POINT('Ctrl Pts',(-16.7250430191669,16.9414525023501,
3.93914446010781));
#209365=CARTESIAN_POINT('Ctrl Pts',(-19.5549199710057,16.2933220883461,
4.06632026678924));
#209366=CARTESIAN_POINT('Ctrl Pts',(-21.6316538014862,18.3219800667756,
4.19349607347067));
#209367=CARTESIAN_POINT('Ctrl Pts',(-21.0499701177813,21.1662586551355,
4.32067188015211));
#209368=CARTESIAN_POINT('Ctrl Pts',(-18.3435275963289,22.2167087844487,
4.44784768683354));
#209369=CARTESIAN_POINT('Ctrl Pts',(-15.995319269794,20.5096076593562,4.57502349351498));
#209370=CARTESIAN_POINT('Ctrl Pts',(-16.1596805315267,17.6111146074862,
4.70219930019641));
#209371=CARTESIAN_POINT('Ctrl Pts',(-18.6858201252975,16.180417103161,4.82937510687785));
#209372=CARTESIAN_POINT('Ctrl Pts',(-21.2561617637275,17.5300913074975,
4.95655091355928));
#209373=CARTESIAN_POINT('Ctrl Pts',(-21.5125765269512,20.4218949082454,
5.08372672024072));
#209374=CARTESIAN_POINT('Ctrl Pts',(-19.2198197846062,22.2027775872924,
5.21090252692215));
#209375=CARTESIAN_POINT('Ctrl Pts',(-16.4813535432613,21.2388900206576,
5.33807833360358));
#209376=CARTESIAN_POINT('Ctrl Pts',(-15.8095506109669,18.4145392251191,
5.46525414028503));
#209377=CARTESIAN_POINT('Ctrl Pts',(-17.8207484813105,16.3208917566031,
5.59242994696645));
#209378=CARTESIAN_POINT('Ctrl Pts',(-20.6697979372697,16.8787392210558,
5.71960575364789));
#209379=CARTESIAN_POINT('Ctrl Pts',(-21.7428729349543,19.5762911937604,
5.84678156032932));
#209380=CARTESIAN_POINT('Ctrl Pts',(-20.0554937665342,21.9387111687183,
5.97395736701076));
#209381=CARTESIAN_POINT('Ctrl Pts',(-17.1557260884723,21.7986254472259,
6.10113317369219));
#209382=CARTESIAN_POINT('Ctrl Pts',(-15.7039267655104,19.284553984052,6.22830898037363));
#209383=CARTESIAN_POINT('Ctrl Pts',(-17.0320315676376,16.7030013057854,
6.35548478705506));
#209384=CARTESIAN_POINT('Ctrl Pts',(-19.9215867703828,16.4223817655062,
6.48266059373649));
#209385=CARTESIAN_POINT('Ctrl Pts',(-21.7216048212496,18.7001463742074,
6.60983640041793));
#209386=CARTESIAN_POINT('Ctrl Pts',(-20.7806808802879,21.4465874774214,
6.73701220709936));
#209387=CARTESIAN_POINT('Ctrl Pts',(-17.9620542630039,22.1420158263089,
6.8641880137808));
#209388=CARTESIAN_POINT('Ctrl Pts',(-15.8516399470578,20.1484190739168,
6.99136382046223));
#209389=CARTESIAN_POINT('Ctrl Pts',(-16.3856120802451,17.2947985039956,
7.11853962714367));
#209390=CARTESIAN_POINT('Ctrl Pts',(-19.0740843724149,16.1991738737805,
7.2457154338251));
#209391=CARTESIAN_POINT('Ctrl Pts',(-21.4505503609105,17.86671277936,7.37289124050654));
#209392=CARTESIAN_POINT('Ctrl Pts',(-21.3347500014016,20.7675517740021,
7.50006704718796));
#209393=CARTESIAN_POINT('Ctrl Pts',(-18.8329229363566,22.2403511264959,
7.62724285386941));
#209394=CARTESIAN_POINT('Ctrl Pts',(-16.2403402170543,20.9339088431657,
7.75441866055083));
#209395=CARTESIAN_POINT('Ctrl Pts',(-15.9355355746231,18.0468046320139,
7.88159446723227));
#209396=CARTESIAN_POINT('Ctrl Pts',(-18.1981483501842,16.2277774128756,
8.0087702739137));
#209397=CARTESIAN_POINT('Ctrl Pts',(-20.952371755747,17.145671757748,8.13594608059513));
#209398=CARTESIAN_POINT('Ctrl Pts',(-21.6713767630913,19.958376576159,8.26312188727658));
#209399=CARTESIAN_POINT('Ctrl Pts',(-19.6955209044624,22.0854097733659,
8.390297693958));
#209400=CARTESIAN_POINT('Ctrl Pts',(-16.8375292947071,21.5753504095007,
8.51747350063944));
#209401=CARTESIAN_POINT('Ctrl Pts',(-15.719431848811,18.896146293055,8.64464930732087));
#209402=CARTESIAN_POINT('Ctrl Pts',(-17.3670135764298,16.5058009107065,
8.77182511400231));
#209403=CARTESIAN_POINT('Ctrl Pts',(-20.268720502928,16.5973077891932,8.89900092068374));
#209404=CARTESIAN_POINT('Ctrl Pts',(-21.7624166234869,19.0867150470611,
9.02617672736517));
#209405=CARTESIAN_POINT('Ctrl Pts',(-20.4777284567308,21.6901460352563,
9.15335253404662));
#209406=CARTESIAN_POINT('Ctrl Pts',(-17.5932776589179,22.0191144092604,
9.28052834072804));
#209407=CARTESIAN_POINT('Ctrl Pts',(-15.7553688078344,19.7718121040047,
9.40770414740949));
#209408=CARTESIAN_POINT('Ctrl Pts',(-16.6501692008611,17.0099995012495,
9.53487995409091));
#209409=CARTESIAN_POINT('Ctrl Pts',(-19.4567550149717,16.2674682466002,
9.66205576077236));
#209410=CARTESIAN_POINT('Ctrl Pts',(-21.6002579620812,18.2254446795103,
9.78923156745378));
#209411=CARTESIAN_POINT('Ctrl Pts',(-21.1141471290137,21.0876069485077,
9.91640737413522));
#209412=CARTESIAN_POINT('Ctrl Pts',(-18.4443990336675,22.2280988176125,
10.0435831808167));
#209413=CARTESIAN_POINT('Ctrl Pts',(-16.0403418502683,20.6005897838297,
10.1707589874981));
#209414=CARTESIAN_POINT('Ctrl Pts',(-16.1075488319678,17.698218371052,10.2979347941796));
#209415=CARTESIAN_POINT('Ctrl Pts',(-18.5843617443927,16.183730209017,10.425110600861));
#209416=CARTESIAN_POINT('Ctrl Pts',(-21.1984584687395,17.4465741866552,
10.5522864075424));
#209417=CARTESIAN_POINT('Ctrl Pts',(-21.5515675095613,20.3281693354206,
10.6794622142238));
#209418=CARTESIAN_POINT('Ctrl Pts',(-19.3197332383227,22.1848309582866,
10.8066380209053));
#209419=CARTESIAN_POINT('Ctrl Pts',(-16.5505250756278,21.3131872536903,
10.9338138275867));
#209420=CARTESIAN_POINT('Ctrl Pts',(-15.7845196343066,18.5129172202892,
11.0609896342681));
#209421=CARTESIAN_POINT('Ctrl Pts',(-17.7244793631115,16.3530948093689,
11.1881654409496));
#209422=CARTESIAN_POINT('Ctrl Pts',(-20.5906116183444,16.8152230292517,
11.315341247631));
#209423=CARTESIAN_POINT('Ctrl Pts',(-21.7534179480593,19.4753279211071,
11.4425170543125));
#209424=CARTESIAN_POINT('Ctrl Pts',(-20.1460957166431,21.8929283513879,
11.5696928609939));
#209425=CARTESIAN_POINT('Ctrl Pts',(-17.2432633097514,21.8500259785168,
11.6968686676753));
#209426=CARTESIAN_POINT('Ctrl Pts',(-15.7080892906089,19.3859810667816,
11.8240444743568));
#209427=CARTESIAN_POINT('Ctrl Pts',(-16.9490005381331,16.7614018868241,
11.9512202810382));
#209428=CARTESIAN_POINT('Ctrl Pts',(-19.8275380023589,16.3841769364998,
12.0783960877196));
#209429=CARTESIAN_POINT('Ctrl Pts',(-21.7028222220433,18.6003866945102,
12.205571894401));
#209430=CARTESIAN_POINT('Ctrl Pts',(-20.8543963188915,21.3767962613715,
12.3327477010825));
#209431=CARTESIAN_POINT('Ctrl Pts',(-18.0606383997947,22.1662221829007,
12.4599235077639));
#209432=CARTESIAN_POINT('Ctrl Pts',(-15.8846479553519,20.2444151733933,
12.5870993144454));
#209433=CARTESIAN_POINT('Ctrl Pts',(-16.3227611611408,17.3745138832769,
12.7142751211268));
#209434=CARTESIAN_POINT('Ctrl Pts',(-18.9730363432223,16.1894746200704,
12.8414509278082));
#209435=CARTESIAN_POINT('Ctrl Pts',(-21.4040105166661,17.776497355934,12.9686267344897));
#209436=CARTESIAN_POINT('Ctrl Pts',(-21.385415760611,20.6795872324527,13.0958025411711));
#209437=CARTESIAN_POINT('Ctrl Pts',(-18.934311609617,22.2353394739996,13.2229783478525));
#209438=CARTESIAN_POINT('Ctrl Pts',(-16.2994339895399,21.0164479598295,
13.350154154534));
#209439=CARTESIAN_POINT('Ctrl Pts',(-15.8981195778518,18.1411700012542,
13.4773299612154));
#209440=CARTESIAN_POINT('Ctrl Pts',(-18.0985494388948,16.2473946653896,
13.6045057678968));
#209441=CARTESIAN_POINT('Ctrl Pts',(-20.881965749242,17.0725432819383,13.7316815745783));
#209442=CARTESIAN_POINT('Ctrl Pts',(-21.6947568024494,19.8595932097158,
13.8588573812597));
#209443=CARTESIAN_POINT('Ctrl Pts',(-19.7912372547015,22.0515991238136,
13.9860331879411));
#209444=CARTESIAN_POINT('Ctrl Pts',(-16.9177681453095,21.6375316492779,
14.1132089946226));
#209445=CARTESIAN_POINT('Ctrl Pts',(-15.7105790345338,18.9972719940692,
14.240384801304));
#209446=CARTESIAN_POINT('Ctrl Pts',(-17.2771910049047,16.5530945188459,
14.3675606079854));
#209447=CARTESIAN_POINT('Ctrl Pts',(-20.1803348085118,16.5473803543624,
14.4947364146669));
#209448=CARTESIAN_POINT('Ctrl Pts',(-21.7565561949717,18.9853718918711,
14.6219122213483));
#209449=CARTESIAN_POINT('Ctrl Pts',(-20.5597698735399,21.6303632145285,
14.7490880280298));
#209450=CARTESIAN_POINT('Ctrl Pts',(-17.6879530131938,22.0557389504721,
14.8762638347112));
#209451=CARTESIAN_POINT('Ctrl Pts',(-15.7758193382441,19.8712432637697,
15.0034396413926));
#209452=CARTESIAN_POINT('Ctrl Pts',(-16.5776328150568,17.081015361877,15.130615448074));
#209453=CARTESIAN_POINT('Ctrl Pts',(-19.3577793448131,16.244916163706,15.2577912547555));
#209454=CARTESIAN_POINT('Ctrl Pts',(-21.5656470418159,18.1300147894097,
15.3849670614369));
#209455=CARTESIAN_POINT('Ctrl Pts',(-21.1756543297891,21.006850252321,15.5121428681183));
#209456=CARTESIAN_POINT('Ctrl Pts',(-18.5455953163398,22.2361045717652,
15.6393186747998));
#209457=CARTESIAN_POINT('Ctrl Pts',(-16.0883859064352,20.6900132057797,
15.7664944814812));
#209458=CARTESIAN_POINT('Ctrl Pts',(-16.0583632220467,17.7870190214039,
15.8936702881626));
#209459=CARTESIAN_POINT('Ctrl Pts',(-18.4830712126828,16.1904390026627,
16.0208460948441));
#209460=CARTESIAN_POINT('Ctrl Pts',(-21.1379907912854,17.3650362218196,
16.1480219015255));
#209461=CARTESIAN_POINT('Ctrl Pts',(-21.5873980273796,20.2331906340233,
16.2751977082069));
#209462=CARTESIAN_POINT('Ctrl Pts',(-19.418989675208,22.1635485838168,16.4023735148884));
#209463=CARTESIAN_POINT('Ctrl Pts',(-16.6221458112869,21.3851264637907,
16.5295493215698));
#209464=CARTESIAN_POINT('Ctrl Pts',(-15.7627970890565,18.6120782547437,
16.6567251282513));
#209465=CARTESIAN_POINT('Ctrl Pts',(-17.629342623966,16.3885035736934,16.7839009349327));
#209466=CARTESIAN_POINT('Ctrl Pts',(-20.5093427386175,16.7543941798941,
16.9110767416142));
#209467=CARTESIAN_POINT('Ctrl Pts',(-21.7605760807848,19.374068151889,17.0382525482955));
#209468=CARTESIAN_POINT('Ctrl Pts',(-20.2351137193294,21.8441372156765,
17.165428354977));
#209469=CARTESIAN_POINT('Ctrl Pts',(-17.3324726900139,21.8984663150084,
17.2926041616584));
#209470=CARTESIAN_POINT('Ctrl Pts',(-15.7156459790158,19.4872118732907,
17.4197799683399));
#209471=CARTESIAN_POINT('Ctrl Pts',(-16.8679717420912,16.8225501814725,
17.5469557750213));
#209472=CARTESIAN_POINT('Ctrl Pts',(-19.7322626130239,16.3491429542363,
17.6741315817028));
#209473=CARTESIAN_POINT('Ctrl Pts',(-21.6807094956696,18.501311939612,17.8013073883841));
#209474=CARTESIAN_POINT('Ctrl Pts',(-20.925733309462,21.3045756721761,17.9284831950656));
#209475=CARTESIAN_POINT('Ctrl Pts',(-18.1599778461229,22.1871136674968,
18.055659001747));
#209476=CARTESIAN_POINT('Ctrl Pts',(-15.9208520811544,20.3392520913025,
18.1828348084285));
#209477=CARTESIAN_POINT('Ctrl Pts',(-16.2626149280343,17.4562892486245,
18.3100106151099));
#209478=CARTESIAN_POINT('Ctrl Pts',(-18.8717201870645,16.1831646105782,
18.4371864217913));
#209479=CARTESIAN_POINT('Ctrl Pts',(-21.3544757221902,17.6878910139056,
18.5643622284728));
#209480=CARTESIAN_POINT('Ctrl Pts',(-21.4331074275647,20.5899753767109,
18.6915380351542));
#209481=CARTESIAN_POINT('Ctrl Pts',(-19.0354755930861,22.226935421132,18.8187138418356));
#209482=CARTESIAN_POINT('Ctrl Pts',(-16.3612586147209,21.0969619050252,
18.9458896485171));
#209483=CARTESIAN_POINT('Ctrl Pts',(-15.8638845863206,18.2367354003361,
19.0730654551985));
#209484=CARTESIAN_POINT('Ctrl Pts',(-17.9996633145444,16.2703361898353,
19.20024126188));
#209485=CARTESIAN_POINT('Ctrl Pts',(-20.8091503658403,17.0018135191641,
19.3274170685614));
#209486=CARTESIAN_POINT('Ctrl Pts',(-21.7148157697857,19.7600823036045,
19.4545928752428));
#209487=CARTESIAN_POINT('Ctrl Pts',(-19.8857676864347,22.0146021996221,
19.5817686819242));
#209488=CARTESIAN_POINT('Ctrl Pts',(-17.000044293062,21.6969910014797,19.7089444886057));
#209489=CARTESIAN_POINT('Ctrl Pts',(-15.7051175323933,19.0986375254879,
19.8361202952871));
#209490=CARTESIAN_POINT('Ctrl Pts',(-17.1890026482639,16.6033693221106,
19.9632961019685));
#209491=CARTESIAN_POINT('Ctrl Pts',(-20.0903265437325,16.500441041753,20.09047190865));
#209492=CARTESIAN_POINT('Ctrl Pts',(-21.7473057839905,18.8842811671185,
20.2176477153314));
#209493=CARTESIAN_POINT('Ctrl Pts',(-20.6397625190695,21.5678678598662,
20.3448235220129));
#209494=CARTESIAN_POINT('Ctrl Pts',(-17.7838032706328,22.0891701106396,
20.4719993286943));
#209495=CARTESIAN_POINT('Ctrl Pts',(-15.7995850674674,19.9699385269971,
20.5991751353757));
#209496=CARTESIAN_POINT('Ctrl Pts',(-16.5075209908883,17.1544113723013,
20.7263509420572));
#209497=CARTESIAN_POINT('Ctrl Pts',(-19.2580928720921,16.2257085824946,
20.8535267487386));
#209498=CARTESIAN_POINT('Ctrl Pts',(-21.5278812718071,18.035763821068,20.98070255542));
#209499=CARTESIAN_POINT('Ctrl Pts',(-21.2343814736918,20.9241439362665,
21.1078783621014));
#209500=CARTESIAN_POINT('Ctrl Pts',(-18.6470824304151,22.2405922216597,
21.2350541687829));
#209501=CARTESIAN_POINT('Ctrl Pts',(-16.1392443426422,20.7780182314604,
21.3622299754643));
#209502=CARTESIAN_POINT('Ctrl Pts',(-16.0124742037318,17.876952967467,21.4894057821458));
#209503=CARTESIAN_POINT('Ctrl Pts',(-18.381492069836,16.2014330842265,21.6165815888272));
#209504=CARTESIAN_POINT('Ctrl Pts',(-21.0759343030523,17.2838114902333,
21.7437573955087));
#209505=CARTESIAN_POINT('Ctrl Pts',(-21.6178060723067,20.1407222466758,
21.87093320219));
#209506=CARTESIAN_POINT('Ctrl Pts',(-20.221009817676,21.4665545621232,21.955717073311));
#209507=CARTESIAN_POINT('Ctrl Pts',(-19.3965839026516,21.687158879832,21.9981090088715));
#209508=CARTESIAN_POINT('Ctrl Pts',(-17.1140743056112,20.5739122292573,
-2.78423117894278E-16));
#209509=CARTESIAN_POINT('Ctrl Pts',(-17.0603911325521,20.522111673172,-4.4535200385995E-15));
#209510=CARTESIAN_POINT('Ctrl Pts',(-17.0098645202578,20.4674385257497,
1.04642875463197E-14));
#209511=CARTESIAN_POINT('Ctrl Pts',(-16.9624881995608,20.410264093257,-4.6525283625698E-15));
#209512=CARTESIAN_POINT('Ctrl Pts',(-16.9134245654311,20.3510533863865,
-2.03077315114503E-14));
#209513=CARTESIAN_POINT('Ctrl Pts',(-16.8677391100142,20.2891596196025,
-4.05979361674585E-15));
#209514=CARTESIAN_POINT('Ctrl Pts',(-16.8254532095209,20.2249455930866,
-3.18148285494146E-15));
#209515=CARTESIAN_POINT('Ctrl Pts',(-16.7853187213456,20.1639986330401,
-2.34785858603208E-15));
#209516=CARTESIAN_POINT('Ctrl Pts',(-16.7482466106958,20.1009605704111,
-1.98929216896175E-14));
#209517=CARTESIAN_POINT('Ctrl Pts',(-16.7142836213594,20.0361088469223,
-1.85407245112401E-14));
#209518=CARTESIAN_POINT('Ctrl Pts',(-16.6991853089609,20.0072788881953,
-1.79558883097759E-14));
#209519=CARTESIAN_POINT('Ctrl Pts',(-16.6847018341336,19.9780901364722,
8.22240768298966E-15));
#209520=CARTESIAN_POINT('Ctrl Pts',(-16.6708392964776,19.9485654278612,
-1.03736463863413E-14));
#209521=CARTESIAN_POINT('Ctrl Pts',(-16.6640109607001,19.9340223024153,
-1.91889155439778E-14));
#209522=CARTESIAN_POINT('Ctrl Pts',(-16.657333302533,19.9193976511972,-3.21445356456926E-15));
#209523=CARTESIAN_POINT('Ctrl Pts',(-16.6508071688394,19.9046941363876,
4.60048665829049E-15));
#209524=CARTESIAN_POINT('Ctrl Pts',(-16.6447949816305,19.8911485536865,
1.18973701611653E-14));
#209525=CARTESIAN_POINT('Ctrl Pts',(-16.6389109256811,19.8775346474983,
-3.87472281196432E-15));
#209526=CARTESIAN_POINT('Ctrl Pts',(-16.6331636045017,19.8638740397009,
-6.0507154842071E-15));
#209527=CARTESIAN_POINT('Ctrl Pts',(-16.6020948019513,19.790027683611,-1.85629496859678E-14));
#209528=CARTESIAN_POINT('Ctrl Pts',(-16.5749612060018,19.7146929635301,
-9.23216762033033E-15));
#209529=CARTESIAN_POINT('Ctrl Pts',(-16.5517844460822,19.6382510185693,
-1.35724764760425E-14));
#209530=CARTESIAN_POINT('Ctrl Pts',(-16.5281813102643,19.5604027940831,
-1.7992632691482E-14));
#209531=CARTESIAN_POINT('Ctrl Pts',(-16.5086814210927,19.4814054223281,
-2.58768124863866E-14));
#209532=CARTESIAN_POINT('Ctrl Pts',(-16.4933485190228,19.4016259047523,
-6.64746035994312E-15));
#209533=CARTESIAN_POINT('Ctrl Pts',(-16.4794162838084,19.329134278635,1.08252826095013E-14));
#209534=CARTESIAN_POINT('Ctrl Pts',(-16.4689247639322,19.2559959244267,
-1.01990454609122E-14));
#209535=CARTESIAN_POINT('Ctrl Pts',(-16.4619555680579,19.1824703462648,
-1.64729341278758E-14));
#209536=CARTESIAN_POINT('Ctrl Pts',(-16.4592976470201,19.1544290650995,
-1.9145684836839E-14));
#209537=CARTESIAN_POINT('Ctrl Pts',(-16.4571524088489,19.1263313551069,
-2.39160590086535E-14));
#209538=CARTESIAN_POINT('Ctrl Pts',(-16.4555257409501,19.0981913259617,
4.73232564246473E-15));
#209539=CARTESIAN_POINT('Ctrl Pts',(-16.4546322610198,19.0827348512285,
2.03445886243926E-14));
#209540=CARTESIAN_POINT('Ctrl Pts',(-16.453895246137,19.0672656072016,8.61144224714149E-16));
#209541=CARTESIAN_POINT('Ctrl Pts',(-16.4533157740873,19.051785924702,-1.2712053631958E-14));
#209542=CARTESIAN_POINT('Ctrl Pts',(-16.4528680721876,19.0398262740765,
-2.31702952227711E-14));
#209543=CARTESIAN_POINT('Ctrl Pts',(-16.452514580052,19.0278636904617,-5.25880506684687E-15));
#209544=CARTESIAN_POINT('Ctrl Pts',(-16.4522557186358,19.0159077924821,
-5.49560397189452E-15));
#209545=CARTESIAN_POINT('Ctrl Pts',(-16.4504488747984,18.9324560332097,
-7.08812930653476E-15));
#209546=CARTESIAN_POINT('Ctrl Pts',(-16.4532438607103,18.8492105138102,
-8.50757505162779E-16));
#209547=CARTESIAN_POINT('Ctrl Pts',(-16.4606969184041,18.7665518702536,
-4.28823643261467E-15));
#209548=CARTESIAN_POINT('Ctrl Pts',(-16.4681357553308,18.6840509430821,
-6.93785445528216E-15));
#209549=CARTESIAN_POINT('Ctrl Pts',(-16.4802145308229,18.6021336503298,
-7.5002128928925E-15));
#209550=CARTESIAN_POINT('Ctrl Pts',(-16.4970385284052,18.5211628277987,
-4.57966997657877E-15));
#209551=CARTESIAN_POINT('Ctrl Pts',(-16.5134762563069,18.4420510505752,
-2.05411160106774E-15));
#209552=CARTESIAN_POINT('Ctrl Pts',(-16.5344435942651,18.3638418295306,
1.67537111895845E-14));
#209553=CARTESIAN_POINT('Ctrl Pts',(-16.5596748813382,18.2867616450374,
2.91433543964104E-15));
#209554=CARTESIAN_POINT('Ctrl Pts',(-16.5700722924092,18.2549981301094,
-2.73628106559942E-15));
#209555=CARTESIAN_POINT('Ctrl Pts',(-16.581194395652,18.2234264109971,-1.52990285076908E-14));
#209556=CARTESIAN_POINT('Ctrl Pts',(-16.5930250854222,18.1920628114276,
-1.0991207943789E-14));
#209557=CARTESIAN_POINT('Ctrl Pts',(-16.5995763500233,18.1746951647716,
-8.76724025831231E-15));
#209558=CARTESIAN_POINT('Ctrl Pts',(-16.6063471420461,18.1573861965041,
-1.48891845053629E-14));
#209559=CARTESIAN_POINT('Ctrl Pts',(-16.6133223339605,18.1401687566554,
-1.25177646026486E-14));
#209560=CARTESIAN_POINT('Ctrl Pts',(-16.6442815008621,18.0637496988806,
-1.82337894072226E-15));
#209561=CARTESIAN_POINT('Ctrl Pts',(-16.6792965711232,17.9890373934243,
-5.44156629526273E-17));
#209562=CARTESIAN_POINT('Ctrl Pts',(-16.7180395276146,17.9162554524269,
-4.19109191795997E-15));
#209563=CARTESIAN_POINT('Ctrl Pts',(-16.7588464280445,17.8395962170884,
-8.5481403039391E-15));
#209564=CARTESIAN_POINT('Ctrl Pts',(-16.8037890252177,17.7650776476886,
8.20107877868703E-15));
#209565=CARTESIAN_POINT('Ctrl Pts',(-16.8525445311818,17.692966664072,1.08801856413265E-14));
#209566=CARTESIAN_POINT('Ctrl Pts',(-16.9013000371459,17.6208556804554,
1.3559292503966E-14));
#209567=CARTESIAN_POINT('Ctrl Pts',(-16.9538690505405,17.5511513968607,
-1.85766771511439E-14));
#209568=CARTESIAN_POINT('Ctrl Pts',(-17.0099820350415,17.4841394296583,
2.60902410786912E-15));
#209569=CARTESIAN_POINT('Ctrl Pts',(-17.0318957421493,17.4579693616242,
1.08023314394969E-14));
#209570=CARTESIAN_POINT('Ctrl Pts',(-17.0543504737559,17.4322101781547,
3.45386508731371E-17));
#209571=CARTESIAN_POINT('Ctrl Pts',(-17.0773320757735,17.4068801208169,
-6.93889390390723E-16));
#209572=CARTESIAN_POINT('Ctrl Pts',(-17.0864638250902,17.3968152117818,
-1.01658935222294E-15));
#209573=CARTESIAN_POINT('Ctrl Pts',(-17.0956795264284,17.3868172601505,
-1.08346130998296E-14));
#209574=CARTESIAN_POINT('Ctrl Pts',(-17.1049759845535,17.376889953632,-9.29811783123569E-15));
#209575=CARTESIAN_POINT('Ctrl Pts',(-17.1654855522993,17.3122742668584,
1.31805477752442E-15));
#209576=CARTESIAN_POINT('Ctrl Pts',(-17.2292149096655,17.2508596682763,
6.852693416406E-15));
#209577=CARTESIAN_POINT('Ctrl Pts',(-17.2958559710253,17.1929205201455,
8.77076189453874E-15));
#209578=CARTESIAN_POINT('Ctrl Pts',(-17.3510488277484,17.1449346832427,
1.03593272105537E-14));
#209579=CARTESIAN_POINT('Ctrl Pts',(-17.4082400420401,17.099332805993,4.61397673449403E-15));
#209580=CARTESIAN_POINT('Ctrl Pts',(-17.467277750751,17.0562847197858,-6.63358257213531E-15));
#209581=CARTESIAN_POINT('Ctrl Pts',(-17.4867746862249,17.042068284606,-1.02232182230849E-14));
#209582=CARTESIAN_POINT('Ctrl Pts',(-17.5064731567169,17.0281304980274,
-1.79912501438622E-14));
#209583=CARTESIAN_POINT('Ctrl Pts',(-17.5263681208433,17.0144778848535,
-3.10862446895044E-15));
#209584=CARTESIAN_POINT('Ctrl Pts',(-17.5422931383847,17.0035495864712,
8.76560179579256E-15));
#209585=CARTESIAN_POINT('Ctrl Pts',(-17.5583454202066,16.9928032530657,
-3.50265831023961E-15));
#209586=CARTESIAN_POINT('Ctrl Pts',(-17.5745064361378,16.9822524120729,
-5.07927033766009E-15));
#209587=CARTESIAN_POINT('Ctrl Pts',(-17.6490341987622,16.9335964008203,
-1.25342314173774E-14));
#209588=CARTESIAN_POINT('Ctrl Pts',(-17.7259441000136,16.8890440749741,
-4.70463702209119E-15));
#209589=CARTESIAN_POINT('Ctrl Pts',(-17.8049552753632,16.8488860377447,
-7.60502771868232E-15));
#209590=CARTESIAN_POINT('Ctrl Pts',(-17.8827964927912,16.8093226406223,
-1.17346642570966E-14));
#209591=CARTESIAN_POINT('Ctrl Pts',(-17.9626778959222,16.774023635519,-1.23541329108695E-14));
#209592=CARTESIAN_POINT('Ctrl Pts',(-18.0443633532837,16.7433042678249,
2.18158824338843E-14));
#209593=CARTESIAN_POINT('Ctrl Pts',(-18.0530581203136,16.7400344355435,
2.54036404748463E-14));
#209594=CARTESIAN_POINT('Ctrl Pts',(-18.0617733522417,16.7368165315127,
-1.30026374349307E-14));
#209595=CARTESIAN_POINT('Ctrl Pts',(-18.0705086335888,16.7336504254972,
1.08246744900953E-14));
#209596=CARTESIAN_POINT('Ctrl Pts',(-19.3965839091052,16.7348410960496,
0.00189100554319172));
#209597=CARTESIAN_POINT('Ctrl Pts',(-20.2210098321597,16.9554454159071,
0.0442829411036698));
#209598=CARTESIAN_POINT('Ctrl Pts',(-21.6178061486211,18.2812774518108,
0.129066812224626));
#209599=CARTESIAN_POINT('Ctrl Pts',(-21.0759342831862,21.1381886893359,
0.25624261890606));
#209600=CARTESIAN_POINT('Ctrl Pts',(-18.3814920744256,22.2205668231227,
0.383418425587494));
#209601=CARTESIAN_POINT('Ctrl Pts',(-16.012474196746,20.5450470987711,0.51059423226893));
#209602=CARTESIAN_POINT('Ctrl Pts',(-16.139244329641,17.6439817266502,0.637770038950362));
#209603=CARTESIAN_POINT('Ctrl Pts',(-18.647082433769,16.1814077892925,0.764945845631799));
#209604=CARTESIAN_POINT('Ctrl Pts',(-21.2343814795738,17.4978560455519,
0.89212165231323));
#209605=CARTESIAN_POINT('Ctrl Pts',(-21.5278812831845,20.386236189992,1.01929745899466));
#209606=CARTESIAN_POINT('Ctrl Pts',(-19.2580928727389,22.1962914237501,
1.1464732656761));
#209607=CARTESIAN_POINT('Ctrl Pts',(-16.5075209839662,21.2675886369871,
1.27364907235753));
#209608=CARTESIAN_POINT('Ctrl Pts',(-15.7995850569884,18.4520614691495,
1.40082487903897));
#209609=CARTESIAN_POINT('Ctrl Pts',(-17.7838032676266,16.3328298801955,
1.5280006857204));
#209610=CARTESIAN_POINT('Ctrl Pts',(-20.6397625254543,16.8541321316718,
1.65517649240184));
#209611=CARTESIAN_POINT('Ctrl Pts',(-21.747305794399,19.5377188342137,1.78235229908327));
#209612=CARTESIAN_POINT('Ctrl Pts',(-20.0903265483327,21.9215589674176,
1.90952810576471));
#209613=CARTESIAN_POINT('Ctrl Pts',(-17.1890026429968,21.8186306868887,
2.03670391244613));
#209614=CARTESIAN_POINT('Ctrl Pts',(-15.7051175219999,19.3233624748623,
2.16387971912757));
#209615=CARTESIAN_POINT('Ctrl Pts',(-17.0000442871287,16.7250089900212,
2.291055525809));
#209616=CARTESIAN_POINT('Ctrl Pts',(-19.8857676903764,16.4073977907608,
2.41823133249044));
#209617=CARTESIAN_POINT('Ctrl Pts',(-21.714815780002,18.6619176945194,2.54540713917187));
#209618=CARTESIAN_POINT('Ctrl Pts',(-20.8091503729495,21.4201864884025,
2.67258294585331));
#209619=CARTESIAN_POINT('Ctrl Pts',(-17.9996633120291,22.1516638202427,
2.79975875253474));
#209620=CARTESIAN_POINT('Ctrl Pts',(-15.8638845764858,20.1852646030015,
2.92693455921618));
#209621=CARTESIAN_POINT('Ctrl Pts',(-16.3612586065907,17.3250380885132,
3.05411036589761));
#209622=CARTESIAN_POINT('Ctrl Pts',(-19.0354755941188,16.1950645685336,
3.18128617257904));
#209623=CARTESIAN_POINT('Ctrl Pts',(-21.4331074368131,17.832024618564,3.30846197926048));
#209624=CARTESIAN_POINT('Ctrl Pts',(-21.3544757311695,20.7341089913131,
3.43563778594192));
#209625=CARTESIAN_POINT('Ctrl Pts',(-18.8717201875366,22.2388353997967,
3.56281359262335));
#209626=CARTESIAN_POINT('Ctrl Pts',(-16.2626149195662,20.9657107573881,
3.68998939930478));
#209627=CARTESIAN_POINT('Ctrl Pts',(-15.9208520715149,18.0827479048318,
3.81716520598622));
#209628=CARTESIAN_POINT('Ctrl Pts',(-18.1599778441559,16.2348863223055,
3.94434101266766));
#209629=CARTESIAN_POINT('Ctrl Pts',(-20.9257333169718,17.11742432065,4.07151681934909));
#209630=CARTESIAN_POINT('Ctrl Pts',(-21.6807095057666,19.9206880628195,
4.19869262603052));
#209631=CARTESIAN_POINT('Ctrl Pts',(-19.7322626164446,22.0728570555698,
4.32586843271195));
#209632=CARTESIAN_POINT('Ctrl Pts',(-16.8679717356974,21.5994498267117,
4.45304423939339));
#209633=CARTESIAN_POINT('Ctrl Pts',(-15.7156459686732,18.934788125763,4.58022004607482));
#209634=CARTESIAN_POINT('Ctrl Pts',(-17.3324726852114,16.5235336757831,
4.70739585275626));
#209635=CARTESIAN_POINT('Ctrl Pts',(-20.2351137244727,16.5778627753009,
4.8345716594377));
#209636=CARTESIAN_POINT('Ctrl Pts',(-21.7605760911555,19.0479318475521,
4.96174746611912));
#209637=CARTESIAN_POINT('Ctrl Pts',(-20.5093427447009,21.6676058285233,
5.08892327280057));
#209638=CARTESIAN_POINT('Ctrl Pts',(-17.6293426201811,22.033496435978,5.216099079482));
#209639=CARTESIAN_POINT('Ctrl Pts',(-15.7627970788757,19.8099217473088,
5.34327488616343));
#209640=CARTESIAN_POINT('Ctrl Pts',(-16.6221458040505,17.0368735287597,
5.47045069284487));
#209641=CARTESIAN_POINT('Ctrl Pts',(-19.4189896775549,16.2584514060663,
5.5976264995263));
#209642=CARTESIAN_POINT('Ctrl Pts',(-21.5873980371568,18.1888093624738,
5.72480230620774));
#209643=CARTESIAN_POINT('Ctrl Pts',(-21.1379907995229,21.0569637845056,
5.85197811288916));
#209644=CARTESIAN_POINT('Ctrl Pts',(-18.4830712118232,22.2315610076874,
5.97915391957061));
#209645=CARTESIAN_POINT('Ctrl Pts',(-16.0583632128787,20.6349809834757,
6.10632972625205));
#209646=CARTESIAN_POINT('Ctrl Pts',(-16.0883858973698,17.7319867891525,
6.23350553293348));
#209647=CARTESIAN_POINT('Ctrl Pts',(-18.545595315694,16.1858954178693,6.36068133961491));
#209648=CARTESIAN_POINT('Ctrl Pts',(-21.1756543381554,17.4151497415253,
6.48785714629635));
#209649=CARTESIAN_POINT('Ctrl Pts',(-21.5656470515186,20.2919852142942,
6.61503295297778));
#209650=CARTESIAN_POINT('Ctrl Pts',(-19.3577793469507,22.1770838464573,
6.74220875965921));
#209651=CARTESIAN_POINT('Ctrl Pts',(-16.577632807668,21.3409846454216,6.86938456634065));
#209652=CARTESIAN_POINT('Ctrl Pts',(-15.7758193281077,18.5507567339681,
6.99656037302208));
#209653=CARTESIAN_POINT('Ctrl Pts',(-17.6879530096092,16.3662610397804,
7.12373617970353));
#209654=CARTESIAN_POINT('Ctrl Pts',(-20.5597698797958,16.7916367771814,
7.25091198638494));
#209655=CARTESIAN_POINT('Ctrl Pts',(-21.7565562053286,19.4366281089017,
7.3780877930664));
#209656=CARTESIAN_POINT('Ctrl Pts',(-20.1803348134679,21.8746196547645,
7.50526359974782));
#209657=CARTESIAN_POINT('Ctrl Pts',(-17.277190999913,21.8689054902615,7.63243940642925));
#209658=CARTESIAN_POINT('Ctrl Pts',(-15.710579024174,19.4247280066634,7.75961521311069));
#209659=CARTESIAN_POINT('Ctrl Pts',(-16.917768139086,16.7844683424076,7.88679101979213));
#209660=CARTESIAN_POINT('Ctrl Pts',(-19.7912372583239,16.3704008664529,
8.01396682647355));
#209661=CARTESIAN_POINT('Ctrl Pts',(-21.6947568125944,18.5624067880616,
8.141142633155));
#209662=CARTESIAN_POINT('Ctrl Pts',(-20.8819657566022,21.3494567253891,
8.26831843983642));
#209663=CARTESIAN_POINT('Ctrl Pts',(-18.0985494367176,22.1746053447652,
8.39549424651787));
#209664=CARTESIAN_POINT('Ctrl Pts',(-15.8981195681347,20.2808300024119,
8.52267005319929));
#209665=CARTESIAN_POINT('Ctrl Pts',(-16.2994339811977,17.4055520339842,
8.64984585988074));
#209666=CARTESIAN_POINT('Ctrl Pts',(-18.9343116103032,16.1866605156374,
8.77702166656217));
#209667=CARTESIAN_POINT('Ctrl Pts',(-21.385415769696,17.7424127625149,8.9041974732436));
#209668=CARTESIAN_POINT('Ctrl Pts',(-21.404010525815,20.6455026489812,9.03137327992503));
#209669=CARTESIAN_POINT('Ctrl Pts',(-18.9730363440416,22.2325253902829,
9.15854908660646));
#209670=CARTESIAN_POINT('Ctrl Pts',(-16.3227611528787,21.0474861230161,
9.28572489328791));
#209671=CARTESIAN_POINT('Ctrl Pts',(-15.8846479455884,18.1775848230658,
9.41290069996933));
#209672=CARTESIAN_POINT('Ctrl Pts',(-18.0606383974872,16.2557778069732,
9.54007650665076));
#209673=CARTESIAN_POINT('Ctrl Pts',(-20.8543963261569,17.0452037312071,
9.66725231333221));
#209674=CARTESIAN_POINT('Ctrl Pts',(-21.7028222322161,19.8216133075819,
9.79442812001364));
#209675=CARTESIAN_POINT('Ctrl Pts',(-19.8275380061061,22.0378230731863,
9.92160392669508));
#209676=CARTESIAN_POINT('Ctrl Pts',(-16.9490005320169,21.6605981215696,
10.0487797333765));
#209677=CARTESIAN_POINT('Ctrl Pts',(-15.7080892802405,19.0360189326189,
10.175955540058));
#209678=CARTESIAN_POINT('Ctrl Pts',(-17.2432633046432,16.5719740124406,
10.3031313467394));
#209679=CARTESIAN_POINT('Ctrl Pts',(-20.1460957214815,16.5290716394223,
10.4303071534208));
#209680=CARTESIAN_POINT('Ctrl Pts',(-21.7534179584054,18.9466720779869,
10.5574829601022));
#209681=CARTESIAN_POINT('Ctrl Pts',(-20.5906116247063,21.6067769789573,
10.6846587667837));
#209682=CARTESIAN_POINT('Ctrl Pts',(-17.7244793596526,22.0689052004239,
10.8118345734651));
#209683=CARTESIAN_POINT('Ctrl Pts',(-15.7845196242002,19.9090827821031,
10.9390103801465));
#209684=CARTESIAN_POINT('Ctrl Pts',(-16.5505250681459,17.1088127391066,
11.066186186828));
#209685=CARTESIAN_POINT('Ctrl Pts',(-19.3197332403295,16.2371690315234,
11.1933619935094));
#209686=CARTESIAN_POINT('Ctrl Pts',(-21.5515675192157,18.0938306607512,
11.3205378001909));
#209687=CARTESIAN_POINT('Ctrl Pts',(-21.1984584771842,20.9754258193904,
11.4477136068723));
#209688=CARTESIAN_POINT('Ctrl Pts',(-18.5843617438802,22.2382698013562,
11.5748894135537));
#209689=CARTESIAN_POINT('Ctrl Pts',(-16.1075488229684,20.7237816341318,
11.7020652202351));
#209690=CARTESIAN_POINT('Ctrl Pts',(-16.0403418410383,17.821410211409,11.8292410269166));
#209691=CARTESIAN_POINT('Ctrl Pts',(-18.4443990326749,16.1939011720493,
11.956416833598));
#209692=CARTESIAN_POINT('Ctrl Pts',(-21.1141471371691,17.3343930450618,
12.0835926402795));
#209693=CARTESIAN_POINT('Ctrl Pts',(-21.6002579719026,20.1965553238665,
12.2107684469609));
#209694=CARTESIAN_POINT('Ctrl Pts',(-19.4567550174485,22.1545317634859,
12.3379442536423));
#209695=CARTESIAN_POINT('Ctrl Pts',(-16.650169193721,21.4120005062925,12.4651200603238));
#209696=CARTESIAN_POINT('Ctrl Pts',(-15.7553687976281,18.6501878940739,
12.5922958670052));
#209697=CARTESIAN_POINT('Ctrl Pts',(-17.593277655009,16.4028855811176,12.7194716736866));
#209698=CARTESIAN_POINT('Ctrl Pts',(-20.4777284627055,16.7318539562487,
12.8466474803681));
#209699=CARTESIAN_POINT('Ctrl Pts',(-21.7624166338639,19.3352849533645,
12.9738232870495));
#209700=CARTESIAN_POINT('Ctrl Pts',(-20.268720508187,21.8246922197625,13.1009990937309));
#209701=CARTESIAN_POINT('Ctrl Pts',(-17.3670135717459,21.9161990985631,
13.2281749004124));
#209702=CARTESIAN_POINT('Ctrl Pts',(-15.7194318384815,19.5258537080241,
13.3553507070938));
#209703=CARTESIAN_POINT('Ctrl Pts',(-16.8375292882087,16.8466495823981,
13.4825265137753));
#209704=CARTESIAN_POINT('Ctrl Pts',(-19.6955209077569,16.3365902167848,
13.6097023204567));
#209705=CARTESIAN_POINT('Ctrl Pts',(-21.6713767731562,18.4636234212799,
13.7368781271381));
#209706=CARTESIAN_POINT('Ctrl Pts',(-20.9523717633484,21.2763282493288,
13.8640539338195));
#209707=CARTESIAN_POINT('Ctrl Pts',(-18.1981483483483,22.1942225973466,
13.991229740501));
#209708=CARTESIAN_POINT('Ctrl Pts',(-15.9355355650343,20.3751953719755,
14.1184055471824));
#209709=CARTESIAN_POINT('Ctrl Pts',(-16.2403402085095,17.4880911509308,
14.2455813538639));
#209710=CARTESIAN_POINT('Ctrl Pts',(-18.8329229366954,16.181648863124,14.3727571605453));
#209711=CARTESIAN_POINT('Ctrl Pts',(-21.334750010313,17.6544482206642,14.4999329672267));
#209712=CARTESIAN_POINT('Ctrl Pts',(-21.450550370219,20.555287225246,14.6271087739081));
#209713=CARTESIAN_POINT('Ctrl Pts',(-19.0740843735804,22.2228261365397,
14.7542845805896));
#209714=CARTESIAN_POINT('Ctrl Pts',(-16.3856120721985,21.1272015025705,
14.881460387271));
#209715=CARTESIAN_POINT('Ctrl Pts',(-15.8516399371812,18.2735809228713,
15.0086361939525));
#209716=CARTESIAN_POINT('Ctrl Pts',(-17.9620542603586,16.2799841636479,
15.1358120006339));
#209717=CARTESIAN_POINT('Ctrl Pts',(-20.7806808873008,16.9754125149182,
15.2629878073153));
#209718=CARTESIAN_POINT('Ctrl Pts',(-21.7216048314868,19.7218536275428,
15.3901636139968));
#209719=CARTESIAN_POINT('Ctrl Pts',(-19.9215867744523,21.9996182440491,
15.5173394206782));
#209720=CARTESIAN_POINT('Ctrl Pts',(-17.0320315618059,21.7189987028083,
15.6445152273596));
#209721=CARTESIAN_POINT('Ctrl Pts',(-15.7039267551279,19.1374460156962,
15.771691034041));
#209722=CARTESIAN_POINT('Ctrl Pts',(-17.1557260830642,16.6233745439076,
15.8988668407225));
#209723=CARTESIAN_POINT('Ctrl Pts',(-20.0554937710623,16.483288821935,16.0260426474039));
#209724=CARTESIAN_POINT('Ctrl Pts',(-21.7428729452643,18.8457088049877,
16.1532184540854));
#209725=CARTESIAN_POINT('Ctrl Pts',(-20.669797943903,21.5432607869357,16.2803942607668));
#209726=CARTESIAN_POINT('Ctrl Pts',(-17.8207484781814,22.1011082533001,
16.4075700674482));
#209727=CARTESIAN_POINT('Ctrl Pts',(-15.8095506009463,20.0074607776102,
16.5347458741296));
#209728=CARTESIAN_POINT('Ctrl Pts',(-16.4813535355424,17.1831099723939,
16.6619216808111));
#209729=CARTESIAN_POINT('Ctrl Pts',(-19.2198197862706,16.2192224024562,
16.7890974874925));
#209730=CARTESIAN_POINT('Ctrl Pts',(-21.5125765364721,18.0001050876052,
16.916273294174));
#209731=CARTESIAN_POINT('Ctrl Pts',(-21.2561617723699,20.8919086982621,
17.0434491008554));
#209732=CARTESIAN_POINT('Ctrl Pts',(-18.6858201251326,22.2415829072234,
17.1706249075368));
#209733=CARTESIAN_POINT('Ctrl Pts',(-16.1596805227059,20.8108853979961,
17.2978007142183));
#209734=CARTESIAN_POINT('Ctrl Pts',(-15.9953192604098,17.9123923361942,
17.4249765208997));
#209735=CARTESIAN_POINT('Ctrl Pts',(-18.3435275949907,16.2052912052522,
17.5521523275811));
#209736=CARTESIAN_POINT('Ctrl Pts',(-21.0499701257169,17.2557413381646,
17.6793281342626));
#209737=CARTESIAN_POINT('Ctrl Pts',(-21.6316538114152,20.1000199362705,
17.806503940944));
#209738=CARTESIAN_POINT('Ctrl Pts',(-19.5549199738189,22.1286779216513,
17.9336797476255));
#209739=CARTESIAN_POINT('Ctrl Pts',(-16.7250430122834,21.4805475054267,
18.0608555543069));
#209740=CARTESIAN_POINT('Ctrl Pts',(-15.7382593970452,18.7502481169883,
18.1880313609883));
#209741=CARTESIAN_POINT('Ctrl Pts',(-17.4998818483857,16.4426599837058,
18.3152071676697));
#209742=CARTESIAN_POINT('Ctrl Pts',(-20.3937311058227,16.6748519928532,
18.4423829743512));
#209743=CARTESIAN_POINT('Ctrl Pts',(-21.7648800881944,19.2338023873838,
18.5695587810326));
#209744=CARTESIAN_POINT('Ctrl Pts',(-20.355384707288,21.7718330069121,18.6967345877141));
#209745=CARTESIAN_POINT('Ctrl Pts',(-17.458369491917,21.9604582855383,18.8239103943955));
#209746=CARTESIAN_POINT('Ctrl Pts',(-15.7316660931769,19.6266262383536,
18.9510862010769));
#209747=CARTESIAN_POINT('Ctrl Pts',(-16.7594177080439,16.911482913106,19.0782620077583));
#209748=CARTESIAN_POINT('Ctrl Pts',(-19.5987260194682,16.3060037929748,
19.2054378144398));
#209749=CARTESIAN_POINT('Ctrl Pts',(-21.6447018788134,18.3656783845019,
19.3326136211212));
#209750=CARTESIAN_POINT('Ctrl Pts',(-21.0202894232019,21.2008830991642,
19.4597894278026));
#209751=CARTESIAN_POINT('Ctrl Pts',(-18.298348324308,22.2104935619801,19.5869652344841));
#209752=CARTESIAN_POINT('Ctrl Pts',(-15.9760905994637,20.468254879066,19.7141410411655));
#209753=CARTESIAN_POINT('Ctrl Pts',(-16.1840435721468,17.5725628250384,
19.841316847847));
#209754=CARTESIAN_POINT('Ctrl Pts',(-18.7314233036763,16.1800352894614,
19.9684926545284));
#209755=CARTESIAN_POINT('Ctrl Pts',(-21.2811669856061,17.5682295538539,
20.0956684612098));
#209756=CARTESIAN_POINT('Ctrl Pts',(-21.4940430697286,20.4635641243438,
20.2228442678912));
#209757=CARTESIAN_POINT('Ctrl Pts',(-19.1747509132239,22.2097481144726,
20.3500200745727));
#209758=CARTESIAN_POINT('Ctrl Pts',(-16.4510972110931,21.2047682572431,
20.4771958812541));
#209759=CARTESIAN_POINT('Ctrl Pts',(-15.821865006984,18.370627026472,20.6043716879356));
#209760=CARTESIAN_POINT('Ctrl Pts',(-17.8643361386242,16.3074811285329,
20.731547494617));
#209761=CARTESIAN_POINT('Ctrl Pts',(-20.7046694479571,16.9081233905683,
20.8587233012984));
#209762=CARTESIAN_POINT('Ctrl Pts',(-21.7370366957551,19.6215316486842,
20.9858991079799));
#209763=CARTESIAN_POINT('Ctrl Pts',(-20.0143025394107,21.9582647545422,
21.1130749146613));
#209764=CARTESIAN_POINT('Ctrl Pts',(-17.1169733995615,21.7746258892963,
21.2402507213427));
#209765=CARTESIAN_POINT('Ctrl Pts',(-15.7031597664495,19.2388788584707,
21.3674265280241));
#209766=CARTESIAN_POINT('Ctrl Pts',(-17.0699655633607,16.677825505383,21.4946023347056));
#209767=CARTESIAN_POINT('Ctrl Pts',(-19.9633972500118,16.4402806602734,
21.621778141387));
#209768=CARTESIAN_POINT('Ctrl Pts',(-21.7289765870023,18.7457048218335,
21.7489539480685));
#209769=CARTESIAN_POINT('Ctrl Pts',(-20.7467662613402,21.4760665062299,
21.8761297547499));
#209770=CARTESIAN_POINT('Ctrl Pts',(-17.9181406714293,22.1321446364483,
22.0033055614313));
#209771=CARTESIAN_POINT('Ctrl Pts',(-15.8372831342433,20.1003769378317,
22.1305000254672));
#209772=CARTESIAN_POINT('Ctrl Pts',(-16.2233209291159,18.2129921341989,
22.2153025539425));
#209773=CARTESIAN_POINT('Ctrl Pts',(-16.7733106534419,17.5599162528134,
22.2577131468574));
#209774=CARTESIAN_POINT('Ctrl Pts',(-19.3578031414673,16.879769673048,-0.0847273919817696));
#209775=CARTESIAN_POINT('Ctrl Pts',(-20.133975749406,17.0874621114807,-0.0423354564212915));
#209776=CARTESIAN_POINT('Ctrl Pts',(-21.4490181436218,18.3356937357163,
0.0424484146996647));
#209777=CARTESIAN_POINT('Ctrl Pts',(-20.9388618188364,21.0253911164874,
0.169624221381099));
#209778=CARTESIAN_POINT('Ctrl Pts',(-18.402124220429,22.0444180968188,0.296800028062534));
#209779=CARTESIAN_POINT('Ctrl Pts',(-16.1717639989072,20.466965862803,0.423975834743968));
#209780=CARTESIAN_POINT('Ctrl Pts',(-16.291114327307,17.7356986710373,0.551151641425402));
#209781=CARTESIAN_POINT('Ctrl Pts',(-18.6521696836906,16.3587285934148,
0.678327448106838));
#209782=CARTESIAN_POINT('Ctrl Pts',(-21.0880351650422,17.5981256668252,
0.805503254788269));
#209783=CARTESIAN_POINT('Ctrl Pts',(-21.3643565441105,20.3174500921447,
0.932679061469706));
#209784=CARTESIAN_POINT('Ctrl Pts',(-19.2274179293257,22.0215635267321,
1.05985486815114));
#209785=CARTESIAN_POINT('Ctrl Pts',(-16.6378358983264,21.1472173376516,
1.18703067483258));
#209786=CARTESIAN_POINT('Ctrl Pts',(-15.9713351742103,18.4964818337432,
1.31420648151401));
#209787=CARTESIAN_POINT('Ctrl Pts',(-17.8394178972337,16.5012880107125,
1.44138228819545));
#209788=CARTESIAN_POINT('Ctrl Pts',(-20.5282190172933,16.9920786527069,
1.56855809487688));
#209789=CARTESIAN_POINT('Ctrl Pts',(-21.5709382276219,19.5185961132746,
1.69573390155831));
#209790=CARTESIAN_POINT('Ctrl Pts',(-20.0109413052122,21.7629110497128,
1.82290970823975));
#209791=CARTESIAN_POINT('Ctrl Pts',(-17.2794307120758,21.6660071197238,
1.95008551492118));
#209792=CARTESIAN_POINT('Ctrl Pts',(-15.8823967857546,19.316785944752,2.07726132160262));
#209793=CARTESIAN_POINT('Ctrl Pts',(-17.101532012187,16.8705130362003,2.20443712828405));
#209794=CARTESIAN_POINT('Ctrl Pts',(-19.8183551942992,16.5714914916967,
2.33161293496548));
#209795=CARTESIAN_POINT('Ctrl Pts',(-21.5403498405985,18.6940552593023,
2.45878874164692));
#209796=CARTESIAN_POINT('Ctrl Pts',(-20.6876926627317,21.2908836986755,
2.58596454832835));
#209797=CARTESIAN_POINT('Ctrl Pts',(-18.0426437407308,21.9795479587692,
2.71314035500979));
#209798=CARTESIAN_POINT('Ctrl Pts',(-16.0318712688937,20.128241290682,2.84031616169122));
#209799=CARTESIAN_POINT('Ctrl Pts',(-16.5001341986149,17.4354226747645,
2.96749196837266));
#209800=CARTESIAN_POINT('Ctrl Pts',(-19.0178303497907,16.3715860469025,
3.09466777505409));
#209801=CARTESIAN_POINT('Ctrl Pts',(-21.275129772553,17.9127354887059,3.22184358173553));
#209802=CARTESIAN_POINT('Ctrl Pts',(-21.2011003487691,20.6449620394061,
3.34901938841696));
#209803=CARTESIAN_POINT('Ctrl Pts',(-18.8636594807816,22.0616174211049,
3.4761951950984));
#209804=CARTESIAN_POINT('Ctrl Pts',(-16.4072640866091,20.8630082479868,
3.60337100177983));
#209805=CARTESIAN_POINT('Ctrl Pts',(-16.0855044795293,18.1487840426529,
3.73054680846126));
#209806=CARTESIAN_POINT('Ctrl Pts',(-18.1935751282717,16.4090770495669,
3.8577226151427));
#209807=CARTESIAN_POINT('Ctrl Pts',(-20.7974520542944,17.2399604565832,
3.98489842182413));
#209808=CARTESIAN_POINT('Ctrl Pts',(-21.50823979277,19.8791503081571,4.11207422850556));
#209809=CARTESIAN_POINT('Ctrl Pts',(-19.6738347101252,21.9053537220903,
4.239250035187));
#209810=CARTESIAN_POINT('Ctrl Pts',(-16.9771896136586,21.4596548264534,
4.36642584186844));
#209811=CARTESIAN_POINT('Ctrl Pts',(-15.8923090067117,18.9509546948064,
4.49360164854987));
#209812=CARTESIAN_POINT('Ctrl Pts',(-17.4145035108715,16.6808299904415,
4.62077745523131));
#209813=CARTESIAN_POINT('Ctrl Pts',(-20.1472541466187,16.7319792297855,
4.74795326191273));
#209814=CARTESIAN_POINT('Ctrl Pts',(-21.5834318192879,19.0574761604191,
4.87512906859417));
#209815=CARTESIAN_POINT('Ctrl Pts',(-20.4054326534448,21.5238216851043,
5.00230487527561));
#209816=CARTESIAN_POINT('Ctrl Pts',(-17.6939977688763,21.8682968636094,
5.12948068195703));
#209817=CARTESIAN_POINT('Ctrl Pts',(-15.9367003815454,19.7748671001969,
5.25665648863848));
#209818=CARTESIAN_POINT('Ctrl Pts',(-16.7457517741515,17.164124269893,5.38383229531991));
#209819=CARTESIAN_POINT('Ctrl Pts',(-19.3788975093713,16.4312628785266,
5.51100810200134));
#209820=CARTESIAN_POINT('Ctrl Pts',(-21.4203898065964,18.2486377661686,
5.63818390868278));
#209821=CARTESIAN_POINT('Ctrl Pts',(-20.9972861924251,20.9489202724142,
5.76535971536421));
#209822=CARTESIAN_POINT('Ctrl Pts',(-18.4977579720875,22.0547687962171,
5.89253552204564));
#209823=CARTESIAN_POINT('Ctrl Pts',(-16.2149671495256,20.5516359536883,
6.01971132872709));
#209824=CARTESIAN_POINT('Ctrl Pts',(-16.2432326184625,17.8185528329019,
6.14688713540851));
#209825=CARTESIAN_POINT('Ctrl Pts',(-18.5566225655012,16.36295356291,6.27406294208995));
#209826=CARTESIAN_POINT('Ctrl Pts',(-21.0327452994073,17.5202601292503,
6.40123874877139));
#209827=CARTESIAN_POINT('Ctrl Pts',(-21.3999118973314,20.2287155878522,
6.52841455545281));
#209828=CARTESIAN_POINT('Ctrl Pts',(-19.3212697946072,22.0034801611529,
6.65559036213426));
#209829=CARTESIAN_POINT('Ctrl Pts',(-16.703844105405,21.2163175074616,6.78276616881569));
#209830=CARTESIAN_POINT('Ctrl Pts',(-15.9489604438082,18.5894005047157,
6.90994197549712));
#209831=CARTESIAN_POINT('Ctrl Pts',(-17.7491777159676,16.5327624580774,
7.03711778217856));
#209832=CARTESIAN_POINT('Ctrl Pts',(-20.4529083087621,16.9332411259839,
7.16429358885998));
#209833=CARTESIAN_POINT('Ctrl Pts',(-21.5796472157492,19.4234221871405,
7.29146939554142));
#209834=CARTESIAN_POINT('Ctrl Pts',(-20.0956814230716,21.7187190760035,
7.41864520222286));
#209835=CARTESIAN_POINT('Ctrl Pts',(-17.3624574402067,21.7133393592328,
7.54582100890429));
#209836=CARTESIAN_POINT('Ctrl Pts',(-15.8875386284201,19.4122185930627,
7.67299681558573));
#209837=CARTESIAN_POINT('Ctrl Pts',(-17.0240714537406,16.9264922567919,
7.80017262226716));
#209838=CARTESIAN_POINT('Ctrl Pts',(-19.7293575901193,16.5366599823728,
7.9273484289486));
#209839=CARTESIAN_POINT('Ctrl Pts',(-21.5214649164229,18.6003686858652,
8.05452423563003));
#209840=CARTESIAN_POINT('Ctrl Pts',(-20.756246191493,21.2242937200225,8.18170004231146));
#209841=CARTESIAN_POINT('Ctrl Pts',(-18.1357421006224,22.0011467251603,
8.3088758489929));
#209842=CARTESIAN_POINT('Ctrl Pts',(-16.0641025003577,20.2182132859998,
8.43605165567432));
#209843=CARTESIAN_POINT('Ctrl Pts',(-16.4419281434871,17.5112241716414,
8.56322746235577));
#209844=CARTESIAN_POINT('Ctrl Pts',(-18.9225874529435,16.3636738798159,
8.6904032690372));
#209845=CARTESIAN_POINT('Ctrl Pts',(-21.2302294793815,17.8283685782694,
8.81757907571863));
#209846=CARTESIAN_POINT('Ctrl Pts',(-21.2477358919618,20.5615417903765,
8.94475488240009));
#209847=CARTESIAN_POINT('Ctrl Pts',(-18.9590456437123,22.0556767338902,
9.07193068908149));
#209848=CARTESIAN_POINT('Ctrl Pts',(-16.4638899852646,20.9399973346102,
9.19910649576295));
#209849=CARTESIAN_POINT('Ctrl Pts',(-16.0514193664187,18.2380701945025,
9.32628230244436));
#209850=CARTESIAN_POINT('Ctrl Pts',(-18.1000499791517,16.4287457641048,
9.45345810912581));
#209851=CARTESIAN_POINT('Ctrl Pts',(-20.7302903886372,17.1719669089676,
9.58063391580724));
#209852=CARTESIAN_POINT('Ctrl Pts',(-21.5290582703031,19.7858743581861,
9.70780972248867));
#209853=CARTESIAN_POINT('Ctrl Pts',(-19.7635336698473,21.8723702644956,
9.83498552917011));
#209854=CARTESIAN_POINT('Ctrl Pts',(-17.0534758273726,21.5172241363981,
9.96216133585154));
#209855=CARTESIAN_POINT('Ctrl Pts',(-15.88519460819,19.0462605035686,10.089337142533));
#209856=CARTESIAN_POINT('Ctrl Pts',(-17.3305155191891,16.7264351338286,
10.2165129492144));
#209857=CARTESIAN_POINT('Ctrl Pts',(-20.0634463312613,16.6860438193137,
10.3436887558959));
#209858=CARTESIAN_POINT('Ctrl Pts',(-21.5766926491464,18.9621430841235,
10.4708645625773));
#209859=CARTESIAN_POINT('Ctrl Pts',(-20.4819448988438,21.466553123448,10.5980403692588));
#209860=CARTESIAN_POINT('Ctrl Pts',(-17.7835661935479,21.9016331674242,
10.7252161759402));
#209861=CARTESIAN_POINT('Ctrl Pts',(-15.9571515150968,19.8682242798172,
10.8523919826216));
#209862=CARTESIAN_POINT('Ctrl Pts',(-16.6783229708898,17.2318529074172,
10.9795677893031));
#209863=CARTESIAN_POINT('Ctrl Pts',(-19.2854505111856,16.4112261527396,
11.1067435959845));
#209864=CARTESIAN_POINT('Ctrl Pts',(-21.3866564343474,18.1592181293605,
11.2339194026659));
#209865=CARTESIAN_POINT('Ctrl Pts',(-21.0542147214219,20.8721546913479,
11.3610952093473));
#209866=CARTESIAN_POINT('Ctrl Pts',(-18.5931200103587,22.0610849269117,
11.4882710160288));
#209867=CARTESIAN_POINT('Ctrl Pts',(-16.261273945793,20.6352391382547,11.6154468227102));
#209868=CARTESIAN_POINT('Ctrl Pts',(-16.1980005612746,17.9027423384994,
11.7426226293916));
#209869=CARTESIAN_POINT('Ctrl Pts',(-18.4613492599099,16.3704907435428,
11.8697984360731));
#209870=CARTESIAN_POINT('Ctrl Pts',(-20.9748380899644,17.4442300894981,
11.9969742427545));
#209871=CARTESIAN_POINT('Ctrl Pts',(-21.4324970545739,20.138871170231,12.124150049436));
#209872=CARTESIAN_POINT('Ctrl Pts',(-19.4144524592281,21.9822480424568,
12.2513258561174));
#209873=CARTESIAN_POINT('Ctrl Pts',(-16.7721349661832,21.2831768387803,
12.3785016627988));
#209874=CARTESIAN_POINT('Ctrl Pts',(-15.9297068745883,18.6830119993224,
12.5056774694802));
#209875=CARTESIAN_POINT('Ctrl Pts',(-17.6600436714977,16.5672433798551,
12.6328532761617));
#209876=CARTESIAN_POINT('Ctrl Pts',(-20.3756687425606,16.876957369329,12.7600290828431));
#209877=CARTESIAN_POINT('Ctrl Pts',(-21.5851646357777,19.3280106054199,
12.8872048895246));
#209878=CARTESIAN_POINT('Ctrl Pts',(-20.1788939389038,21.6717138735354,
13.014380696206));
#209879=CARTESIAN_POINT('Ctrl Pts',(-17.4470227333175,21.7578648918097,
13.1415565028874));
#209880=CARTESIAN_POINT('Ctrl Pts',(-15.8958732910946,19.5074254481115,
13.2687323095689));
#209881=CARTESIAN_POINT('Ctrl Pts',(-16.9485289502823,16.9850340540092,
13.3959081162503));
#209882=CARTESIAN_POINT('Ctrl Pts',(-19.6392434787545,16.5048282563255,
13.5230839229317));
#209883=CARTESIAN_POINT('Ctrl Pts',(-21.4994533012164,18.5073670695018,
13.6502597296132));
#209884=CARTESIAN_POINT('Ctrl Pts',(-20.8225313632018,21.1554454240253,
13.7774355362946));
#209885=CARTESIAN_POINT('Ctrl Pts',(-18.2295115283253,22.0196157878994,
13.904611342976));
#209886=CARTESIAN_POINT('Ctrl Pts',(-16.0993285541244,20.3070554887315,
14.0317871496575));
#209887=CARTESIAN_POINT('Ctrl Pts',(-16.3862931053621,17.5889323075283,
14.1589629563389));
#209888=CARTESIAN_POINT('Ctrl Pts',(-18.8271330173065,16.3589555572926,
14.2861387630203));
#209889=CARTESIAN_POINT('Ctrl Pts',(-21.1825291663591,17.745552565399,14.4133145697018));
#209890=CARTESIAN_POINT('Ctrl Pts',(-21.2915517781366,20.476606638826,14.5404903763832));
#209891=CARTESIAN_POINT('Ctrl Pts',(-19.0541793730395,22.0465451735372,
14.6676661830647));
#209892=CARTESIAN_POINT('Ctrl Pts',(-16.5230622657518,21.0150470053099,
14.7948419897461));
#209893=CARTESIAN_POINT('Ctrl Pts',(-16.0203433033647,18.328447681496,14.9220177964275));
#209894=CARTESIAN_POINT('Ctrl Pts',(-18.0072359316107,16.4515353325348,
15.0491936031089));
#209895=CARTESIAN_POINT('Ctrl Pts',(-20.6608894845385,17.1062605442799,
15.1763694097904));
#209896=CARTESIAN_POINT('Ctrl Pts',(-21.5467415316516,19.6919535717847,
15.3035452164718));
#209897=CARTESIAN_POINT('Ctrl Pts',(-19.8520778019025,21.8364015485223,
15.4307210231533));
#209898=CARTESIAN_POINT('Ctrl Pts',(-17.1316470846427,21.5722065552882,
15.5578968298347));
#209899=CARTESIAN_POINT('Ctrl Pts',(-15.8812757139849,19.1417511005842,
15.6850726365161));
#209900=CARTESIAN_POINT('Ctrl Pts',(-17.2481018157082,16.7748272130226,
15.8122484431975));
#209901=CARTESIAN_POINT('Ctrl Pts',(-19.9781472762768,16.6429406515769,
15.939424249879));
#209902=CARTESIAN_POINT('Ctrl Pts',(-21.5667648313502,18.8670891505701,
16.0666000565604));
#209903=CARTESIAN_POINT('Ctrl Pts',(-20.5564964748742,21.4067545084005,
16.1937758632419));
#209904=CARTESIAN_POINT('Ctrl Pts',(-17.8742007195895,21.9319513886684,
16.3209516699233));
#209905=CARTESIAN_POINT('Ctrl Pts',(-15.9807174389196,19.9608442511223,
16.4481274766047));
#209906=CARTESIAN_POINT('Ctrl Pts',(-16.6132000200527,17.3018015537547,
16.5753032832862));
#209907=CARTESIAN_POINT('Ctrl Pts',(-19.1913849510953,16.3943299325974,
16.7024790899676));
#209908=CARTESIAN_POINT('Ctrl Pts',(-21.3499475780197,18.0709782760214,
16.829654896649));
#209909=CARTESIAN_POINT('Ctrl Pts',(-21.1085406661289,20.7935257934676,
16.9568307033305));
#209910=CARTESIAN_POINT('Ctrl Pts',(-18.6886400736801,22.0642041180355,
17.0840065100119));
#209911=CARTESIAN_POINT('Ctrl Pts',(-16.3103543982751,20.7172447541254,
17.2111823166934));
#209912=CARTESIAN_POINT('Ctrl Pts',(-16.1556131340415,17.9883993163983,
17.3383581233747));
#209913=CARTESIAN_POINT('Ctrl Pts',(-18.3663817865876,16.381214122719,17.4655339300562));
#209914=CARTESIAN_POINT('Ctrl Pts',(-20.9144173329798,17.3701818351261,
17.5927097367376));
#209915=CARTESIAN_POINT('Ctrl Pts',(-21.4620553083253,20.0479859597428,
17.7198855434191));
#209916=CARTESIAN_POINT('Ctrl Pts',(-19.5068718604908,21.9579074155056,
17.8470613501005));
#209917=CARTESIAN_POINT('Ctrl Pts',(-16.8426264504933,21.347711809839,17.9742371567819));
#209918=CARTESIAN_POINT('Ctrl Pts',(-15.9135988802868,18.7772157379466,
18.1014129634634));
#209919=CARTESIAN_POINT('Ctrl Pts',(-17.5721142835804,16.6046898027813,
18.2285887701448));
#209920=CARTESIAN_POINT('Ctrl Pts',(-20.2965877169299,16.8232917077465,
18.3557645768262));
#209921=CARTESIAN_POINT('Ctrl Pts',(-21.5874839051248,19.2324677728927,
18.4829403835077));
#209922=CARTESIAN_POINT('Ctrl Pts',(-20.2604857175586,21.6219484889878,
18.6101161901891));
#209923=CARTESIAN_POINT('Ctrl Pts',(-17.5330316285098,21.7995336065107,
18.7372919968706));
#209924=CARTESIAN_POINT('Ctrl Pts',(-15.9073914798215,19.6022998030865,
18.864467803552));
#209925=CARTESIAN_POINT('Ctrl Pts',(-16.874989209244,17.0460727161496,18.9916436102334));
#209926=CARTESIAN_POINT('Ctrl Pts',(-19.5481139560441,16.4760320435035,
19.1188194169148));
#209927=CARTESIAN_POINT('Ctrl Pts',(-21.4743396776274,18.4151547160267,
19.2459952235963));
#209928=CARTESIAN_POINT('Ctrl Pts',(-20.8864738299528,21.08441604792,19.3731710302777));
#209929=CARTESIAN_POINT('Ctrl Pts',(-18.3238468403057,22.0349344195679,
19.5003468369591));
#209930=CARTESIAN_POINT('Ctrl Pts',(-16.1375099188267,20.3946682605915,
19.6275226436406));
#209931=CARTESIAN_POINT('Ctrl Pts',(-16.3332914883073,17.6684598887888,
19.754698450322));
#209932=CARTESIAN_POINT('Ctrl Pts',(-18.7315741166677,16.3574364254427,
19.8818742570035));
#209933=CARTESIAN_POINT('Ctrl Pts',(-21.1320823343698,17.6643802422104,
20.0090500636849));
#209934=CARTESIAN_POINT('Ctrl Pts',(-21.3324988675726,20.390252053842,20.1362258703664));
#209935=CARTESIAN_POINT('Ctrl Pts',(-19.1489539409205,22.0342326028009,
20.2634016770477));
#209936=CARTESIAN_POINT('Ctrl Pts',(-16.5847145860095,21.0880738092713,
20.3905774837292));
#209937=CARTESIAN_POINT('Ctrl Pts',(-15.9923110877633,18.4198137159881,
20.5177532904106));
#209938=CARTESIAN_POINT('Ctrl Pts',(-17.9152372119337,16.4774229112103,
20.6449290970921));
#209939=CARTESIAN_POINT('Ctrl Pts',(-20.5893269639303,17.0429098251043,
20.7721049037735));
#209940=CARTESIAN_POINT('Ctrl Pts',(-21.5612701751591,19.5975033976856,
20.8992807104549));
#209941=CARTESIAN_POINT('Ctrl Pts',(-19.9393669507179,21.7974684619948,
21.0264565171363));
#209942=CARTESIAN_POINT('Ctrl Pts',(-17.2116173110634,21.6245779050981,
21.1536323238178));
#209943=CARTESIAN_POINT('Ctrl Pts',(-15.8805536168431,19.2372471201844,
21.2808081304992));
#209944=CARTESIAN_POINT('Ctrl Pts',(-17.1673608244619,16.8260911817933,
21.4079839371807));
#209945=CARTESIAN_POINT('Ctrl Pts',(-19.8914411272743,16.6024497401849,
21.535159743862));
#209946=CARTESIAN_POINT('Ctrl Pts',(-21.5536818213048,18.7729383600156,
21.6623355505436));
#209947=CARTESIAN_POINT('Ctrl Pts',(-20.628959867889,21.3434930817089,21.7895113572249));
#209948=CARTESIAN_POINT('Ctrl Pts',(-17.9658925872421,21.9611712248908,
21.9166871639064));
#209949=CARTESIAN_POINT('Ctrl Pts',(-16.0068267982834,20.0483220661474,
22.0438816279422));
#209950=CARTESIAN_POINT('Ctrl Pts',(-16.370269957493,18.2714051300663,22.1286841564175));
#209951=CARTESIAN_POINT('Ctrl Pts',(-16.888069006179,17.6565535153103,22.1710947493324));
#209952=CARTESIAN_POINT('Ctrl Pts',(-19.3190223738293,17.0246982500464,
-0.171345789506731));
#209953=CARTESIAN_POINT('Ctrl Pts',(-20.0469416666524,17.2194788070544,
-0.128953853946253));
#209954=CARTESIAN_POINT('Ctrl Pts',(-21.2802301386225,18.3901100196218,
-0.0441699828252965));
#209955=CARTESIAN_POINT('Ctrl Pts',(-20.8017893544867,20.9125935436388,
0.0830058238561378));
#209956=CARTESIAN_POINT('Ctrl Pts',(-18.4227563664326,21.868269370515,0.210181630537572));
#209957=CARTESIAN_POINT('Ctrl Pts',(-16.3310538010686,20.388884626835,0.337357437219006));
#209958=CARTESIAN_POINT('Ctrl Pts',(-16.4429843249731,17.8274156154244,
0.46453324390044));
#209959=CARTESIAN_POINT('Ctrl Pts',(-18.6572569336122,16.5360493975372,
0.591709050581876));
#209960=CARTESIAN_POINT('Ctrl Pts',(-20.9416888505105,17.6983952880986,
0.718884857263308));
#209961=CARTESIAN_POINT('Ctrl Pts',(-21.2008318050364,20.2486639942973,
0.846060663944744));
#209962=CARTESIAN_POINT('Ctrl Pts',(-19.1967429859123,21.846835629714,0.973236470626179));
#209963=CARTESIAN_POINT('Ctrl Pts',(-16.7681508126867,21.0268460383161,
1.10041227730761));
#209964=CARTESIAN_POINT('Ctrl Pts',(-16.1430852914322,18.540902198337,1.22758808398905));
#209965=CARTESIAN_POINT('Ctrl Pts',(-17.8950325268407,16.6697461412296,
1.35476389067048));
#209966=CARTESIAN_POINT('Ctrl Pts',(-20.4166755091321,17.130025173742,1.48193969735192));
#209967=CARTESIAN_POINT('Ctrl Pts',(-21.3945706608446,19.4994733923354,
1.60911550403335));
#209968=CARTESIAN_POINT('Ctrl Pts',(-19.9315560620918,21.6042631320078,
1.73629131071478));
#209969=CARTESIAN_POINT('Ctrl Pts',(-17.3698587811547,21.5133835525588,
1.86346711739622));
#209970=CARTESIAN_POINT('Ctrl Pts',(-16.0596760495093,19.3102094146417,
1.99064292407765));
#209971=CARTESIAN_POINT('Ctrl Pts',(-17.2030197372453,17.0160170823794,
2.11781873075909));
#209972=CARTESIAN_POINT('Ctrl Pts',(-19.750942698222,16.7355851926327,2.24499453744052));
#209973=CARTESIAN_POINT('Ctrl Pts',(-21.365883901195,18.7261928240851,2.37217034412196));
#209974=CARTESIAN_POINT('Ctrl Pts',(-20.5662349525139,21.1615809089484,
2.49934615080339));
#209975=CARTESIAN_POINT('Ctrl Pts',(-18.0856241694325,21.8074320972958,
2.62652195748482));
#209976=CARTESIAN_POINT('Ctrl Pts',(-16.1998579613017,20.0712179783623,
2.75369776416626));
#209977=CARTESIAN_POINT('Ctrl Pts',(-16.6390097906391,17.5458072610157,
2.8808735708477));
#209978=CARTESIAN_POINT('Ctrl Pts',(-19.0001851054626,16.5481075252713,
3.00804937752912));
#209979=CARTESIAN_POINT('Ctrl Pts',(-21.1171521082928,17.9934463588478,
3.13522518421057));
#209980=CARTESIAN_POINT('Ctrl Pts',(-21.0477249663689,20.5558150874991,
3.26240099089199));
#209981=CARTESIAN_POINT('Ctrl Pts',(-18.8555987740266,21.8843994424129,
3.38957679757343));
#209982=CARTESIAN_POINT('Ctrl Pts',(-16.5519132536521,20.7603057385855,
3.51675260425486));
#209983=CARTESIAN_POINT('Ctrl Pts',(-16.2501568875435,18.214820180474,3.64392841093631));
#209984=CARTESIAN_POINT('Ctrl Pts',(-18.2271724123875,16.5832677768283,
3.77110421761772));
#209985=CARTESIAN_POINT('Ctrl Pts',(-20.6691707916169,17.3624965925164,
3.89828002429917));
#209986=CARTESIAN_POINT('Ctrl Pts',(-21.3357700797732,19.8376125534949,
4.0254558309806));
#209987=CARTESIAN_POINT('Ctrl Pts',(-19.6154068038058,21.7378503886108,
4.15263163766203));
#209988=CARTESIAN_POINT('Ctrl Pts',(-17.0864074916199,21.3198598261951,
4.27980744434348));
#209989=CARTESIAN_POINT('Ctrl Pts',(-16.06897204475,18.9671212638499,4.4069832510249));
#209990=CARTESIAN_POINT('Ctrl Pts',(-17.4965343365317,16.8381263050999,
4.53415905770634));
#209991=CARTESIAN_POINT('Ctrl Pts',(-20.0593945687647,16.8860956842701,
4.66133486438777));
#209992=CARTESIAN_POINT('Ctrl Pts',(-21.4062875474204,19.0670204732863,
4.7885106710692));
#209993=CARTESIAN_POINT('Ctrl Pts',(-20.3015225621888,21.3800375416853,
4.91568647775065));
#209994=CARTESIAN_POINT('Ctrl Pts',(-17.7586529175715,21.7030972912407,
5.04286228443207));
#209995=CARTESIAN_POINT('Ctrl Pts',(-16.1106036842152,19.7398124530851,
5.17003809111352));
#209996=CARTESIAN_POINT('Ctrl Pts',(-16.8693577442526,17.2913750110263,
5.29721389779494));
#209997=CARTESIAN_POINT('Ctrl Pts',(-19.3388053411876,16.604074350987,5.42438970447638));
#209998=CARTESIAN_POINT('Ctrl Pts',(-21.253381576036,18.3084661698633,5.55156551115781));
#209999=CARTESIAN_POINT('Ctrl Pts',(-20.8565815853272,20.8408767603229,
5.67874131783925));
#210000=CARTESIAN_POINT('Ctrl Pts',(-18.5124447323517,21.877976584747,5.80591712452068));
#210001=CARTESIAN_POINT('Ctrl Pts',(-16.3715710861727,20.468290923901,5.93309293120211));
#210002=CARTESIAN_POINT('Ctrl Pts',(-16.3980793395551,17.9051188766514,
6.06026873788356));
#210003=CARTESIAN_POINT('Ctrl Pts',(-18.5676498153085,16.5400117079507,
6.18744454456498));
#210004=CARTESIAN_POINT('Ctrl Pts',(-20.8898362606593,17.6253705169753,
6.31462035124643));
#210005=CARTESIAN_POINT('Ctrl Pts',(-21.2341767431441,20.1654459614101,
6.44179615792784));
#210006=CARTESIAN_POINT('Ctrl Pts',(-19.2847602422637,21.8298764758485,
6.56897196460929));
#210007=CARTESIAN_POINT('Ctrl Pts',(-16.8300554031422,21.0916503695018,
6.69614777129072));
#210008=CARTESIAN_POINT('Ctrl Pts',(-16.1221015595086,18.6280442754634,
6.82332357797216));
#210009=CARTESIAN_POINT('Ctrl Pts',(-17.8104024223259,16.6992638763745,
6.95049938465359));
#210010=CARTESIAN_POINT('Ctrl Pts',(-20.3460467377283,17.0748454747864,
7.07767519133502));
#210011=CARTESIAN_POINT('Ctrl Pts',(-21.4027382261697,19.4102162653792,
7.20485099801646));
#210012=CARTESIAN_POINT('Ctrl Pts',(-20.0110280326754,21.5628184972425,
7.33202680469789));
#210013=CARTESIAN_POINT('Ctrl Pts',(-17.4477238805002,21.5577732282041,
7.45920261137933));
#210014=CARTESIAN_POINT('Ctrl Pts',(-16.0644982326662,19.3997091794621,
7.58637841806076));
#210015=CARTESIAN_POINT('Ctrl Pts',(-17.1303747683952,17.0685161711762,
7.7135542247422));
#210016=CARTESIAN_POINT('Ctrl Pts',(-19.6674779219145,16.7029190982927,
7.84073003142363));
#210017=CARTESIAN_POINT('Ctrl Pts',(-21.3481730202512,18.6383305836686,
7.96790583810506));
#210018=CARTESIAN_POINT('Ctrl Pts',(-20.6305266263839,21.0991307146561,
8.0950816447865));
#210019=CARTESIAN_POINT('Ctrl Pts',(-18.1729347645271,21.8276881055553,
8.22225745146793));
#210020=CARTESIAN_POINT('Ctrl Pts',(-16.2300854325808,20.1555965695878,
8.34943325814937));
#210021=CARTESIAN_POINT('Ctrl Pts',(-16.5844223057765,17.6168963092987,
8.4766090648308));
#210022=CARTESIAN_POINT('Ctrl Pts',(-18.9108632955837,16.5406872439944,
8.60378487151224));
#210023=CARTESIAN_POINT('Ctrl Pts',(-21.075043189067,17.9143243940239,8.73096067819366));
#210024=CARTESIAN_POINT('Ctrl Pts',(-21.0914612581086,20.4775809317718,
8.85813648487511));
#210025=CARTESIAN_POINT('Ctrl Pts',(-18.945054943383,21.8788280774976,8.98531229155654));
#210026=CARTESIAN_POINT('Ctrl Pts',(-16.6050188176507,20.8325085462043,
9.11248809823798));
#210027=CARTESIAN_POINT('Ctrl Pts',(-16.218190787249,18.2985555659393,9.23966390491941));
#210028=CARTESIAN_POINT('Ctrl Pts',(-18.1394615608164,16.6017137212363,
9.36683971160084));
#210029=CARTESIAN_POINT('Ctrl Pts',(-20.6061844511175,17.2987300867281,
9.49401551828229));
#210030=CARTESIAN_POINT('Ctrl Pts',(-21.3552943083903,19.7501354087903,
9.62119132496371));
#210031=CARTESIAN_POINT('Ctrl Pts',(-19.6995293335885,21.7069174558048,
9.74836713164515));
#210032=CARTESIAN_POINT('Ctrl Pts',(-17.1579511227282,21.3738501512268,
9.87554293832658));
#210033=CARTESIAN_POINT('Ctrl Pts',(-16.0622999361394,19.0565020745182,
10.002718745008));
#210034=CARTESIAN_POINT('Ctrl Pts',(-17.4177677337352,16.8808962552165,
10.1298945516894));
#210035=CARTESIAN_POINT('Ctrl Pts',(-19.980796941041,16.8430159992049,10.2570703583709));
#210036=CARTESIAN_POINT('Ctrl Pts',(-21.3999673398873,18.9776140902601,
10.3842461650523));
#210037=CARTESIAN_POINT('Ctrl Pts',(-20.3732781729815,21.3263292679386,
10.5114219717337));
#210038=CARTESIAN_POINT('Ctrl Pts',(-17.8426530274432,21.7343611344247,
10.6385977784151));
#210039=CARTESIAN_POINT('Ctrl Pts',(-16.1297834059934,19.8273657775314,
10.7657735850966));
#210040=CARTESIAN_POINT('Ctrl Pts',(-16.8061208736337,17.3548930757276,
10.892949391778));
#210041=CARTESIAN_POINT('Ctrl Pts',(-19.2511677820415,16.5852832739556,
11.0201251984594));
#210042=CARTESIAN_POINT('Ctrl Pts',(-21.2217453494789,18.2246055979698,
11.1473010051409));
#210043=CARTESIAN_POINT('Ctrl Pts',(-20.9099709656597,20.7688835633054,
11.2744768118223));
#210044=CARTESIAN_POINT('Ctrl Pts',(-18.6018782768372,21.8839000524673,
11.4016526185037));
#210045=CARTESIAN_POINT('Ctrl Pts',(-16.4149990686176,20.5466966423776,
11.5288284251852));
#210046=CARTESIAN_POINT('Ctrl Pts',(-16.3556592815108,17.9840744655897,
11.6560042318666));
#210047=CARTESIAN_POINT('Ctrl Pts',(-18.4782994871448,16.5470803150364,
11.783180038548));
#210048=CARTESIAN_POINT('Ctrl Pts',(-20.8355290427597,17.5540671339344,
11.9103558452295));
#210049=CARTESIAN_POINT('Ctrl Pts',(-21.2647361372453,20.0811870165956,
12.0375316519109));
#210050=CARTESIAN_POINT('Ctrl Pts',(-19.3721499010078,21.8099643214279,
12.1647074585924));
#210051=CARTESIAN_POINT('Ctrl Pts',(-16.8941007386454,21.1543531712681,
12.2918832652738));
#210052=CARTESIAN_POINT('Ctrl Pts',(-16.1040449515487,18.7158361045709,
12.4190590719552));
#210053=CARTESIAN_POINT('Ctrl Pts',(-17.7268096879865,16.7316011785925,
12.5462348786367));
#210054=CARTESIAN_POINT('Ctrl Pts',(-20.2736090224157,17.0220607824092,
12.6734106853181));
#210055=CARTESIAN_POINT('Ctrl Pts',(-21.4079126376915,19.3207362574753,
12.8005864919995));
#210056=CARTESIAN_POINT('Ctrl Pts',(-20.0890673696206,21.5187355273081,
12.9277622986809));
#210057=CARTESIAN_POINT('Ctrl Pts',(-17.5270318948891,21.5995306850564,
13.0549381053624));
#210058=CARTESIAN_POINT('Ctrl Pts',(-16.0723147437075,19.4889971881991,
13.1821139120438));
#210059=CARTESIAN_POINT('Ctrl Pts',(-17.0595286123559,17.1234185256205,
13.3092897187253));
#210060=CARTESIAN_POINT('Ctrl Pts',(-19.5829660497523,16.6730662958661,
13.4364655254067));
#210061=CARTESIAN_POINT('Ctrl Pts',(-21.3275298292767,18.5511107177236,
13.5636413320881));
#210062=CARTESIAN_POINT('Ctrl Pts',(-20.6926909630551,21.0345625987219,
13.6908171387696));
#210063=CARTESIAN_POINT('Ctrl Pts',(-18.2608747083023,21.8450089784522,
13.817992945451));
#210064=CARTESIAN_POINT('Ctrl Pts',(-16.2631215432146,20.2389156054877,
13.9451687521324));
#210065=CARTESIAN_POINT('Ctrl Pts',(-16.5322460022147,17.6897734641258,
14.0723445588139));
#210066=CARTESIAN_POINT('Ctrl Pts',(-18.8213430979177,16.5362622514614,
14.1995203654953));
#210067=CARTESIAN_POINT('Ctrl Pts',(-21.0303083224052,17.8366569101336,
14.3266961721767));
#210068=CARTESIAN_POINT('Ctrl Pts',(-21.1325531860542,20.3979260524059,
14.4538719788582));
#210069=CARTESIAN_POINT('Ctrl Pts',(-19.0342743724987,21.8702642105349,
14.5810477855396));
#210070=CARTESIAN_POINT('Ctrl Pts',(-16.6605124593049,20.9028925080494,
14.708223592221));
#210071=CARTESIAN_POINT('Ctrl Pts',(-16.1890466695481,18.3833144401207,
14.8353993989025));
#210072=CARTESIAN_POINT('Ctrl Pts',(-18.0524176028627,16.6230865014217,
14.9625752055839));
#210073=CARTESIAN_POINT('Ctrl Pts',(-20.5410980817764,17.2371085736416,
15.0897510122653));
#210074=CARTESIAN_POINT('Ctrl Pts',(-21.3718782318164,19.6620535160264,
15.2169268189468));
#210075=CARTESIAN_POINT('Ctrl Pts',(-19.7825688293528,21.6731848529956,
15.3441026256282));
#210076=CARTESIAN_POINT('Ctrl Pts',(-17.2312626074793,21.4254144077681,
15.4712784323096));
#210077=CARTESIAN_POINT('Ctrl Pts',(-16.0586246728421,19.1460561854722,
15.5984542389911));
#210078=CARTESIAN_POINT('Ctrl Pts',(-17.3404775483521,16.9262798821378,
15.7256300456725));
#210079=CARTESIAN_POINT('Ctrl Pts',(-19.9008007814914,16.8025924812187,
15.852805852354));
#210080=CARTESIAN_POINT('Ctrl Pts',(-21.3906567174362,18.8884694961524,
15.9799816590354));
#210081=CARTESIAN_POINT('Ctrl Pts',(-20.4431950058454,21.2702482298655,
16.1071574657168));
#210082=CARTESIAN_POINT('Ctrl Pts',(-17.9276529609976,21.7627945240366,
16.2343332723983));
#210083=CARTESIAN_POINT('Ctrl Pts',(-16.1518842768929,19.9142277246345,
16.3615090790797));
#210084=CARTESIAN_POINT('Ctrl Pts',(-16.7450465045628,17.4204931351153,
16.4886848857611));
#210085=CARTESIAN_POINT('Ctrl Pts',(-19.1629501159199,16.5694374627385,
16.6158606924426));
#210086=CARTESIAN_POINT('Ctrl Pts',(-21.1873186195673,18.1418514644375,
16.743036499124));
#210087=CARTESIAN_POINT('Ctrl Pts',(-20.960919559888,20.6951428886731,16.8702123058054));
#210088=CARTESIAN_POINT('Ctrl Pts',(-18.6914600222275,21.8868253288476,
16.9973881124868));
#210089=CARTESIAN_POINT('Ctrl Pts',(-16.4610282738444,20.6236041102547,
17.1245639191683));
#210090=CARTESIAN_POINT('Ctrl Pts',(-16.3159070076732,18.0644062966023,
17.2517397258497));
#210091=CARTESIAN_POINT('Ctrl Pts',(-18.3892359781844,16.5571370401859,
17.3789155325312));
#210092=CARTESIAN_POINT('Ctrl Pts',(-20.7788645402429,17.4846223320876,
17.5060913392126));
#210093=CARTESIAN_POINT('Ctrl Pts',(-21.2924568052356,19.9959519832151,
17.633267145894));
#210094=CARTESIAN_POINT('Ctrl Pts',(-19.4588237471628,21.78713690936,17.7604429525755));
#210095=CARTESIAN_POINT('Ctrl Pts',(-16.9602098887033,21.2148761142513,
17.8876187592569));
#210096=CARTESIAN_POINT('Ctrl Pts',(-16.0889383635284,18.8041833589049,
18.0147945659384));
#210097=CARTESIAN_POINT('Ctrl Pts',(-17.6443467187751,16.7667196218568,
18.1419703726198));
#210098=CARTESIAN_POINT('Ctrl Pts',(-20.199444328037,16.97173142264,18.2691461793012));
#210099=CARTESIAN_POINT('Ctrl Pts',(-21.410087722055,19.2311331584014,18.3963219859826));
#210100=CARTESIAN_POINT('Ctrl Pts',(-20.1655867278293,21.4720639710636,
18.5234977926641));
#210101=CARTESIAN_POINT('Ctrl Pts',(-17.6076937651026,21.638608927483,18.6506735993455));
#210102=CARTESIAN_POINT('Ctrl Pts',(-16.083116866466,19.5779733678196,18.777849406027));
#210103=CARTESIAN_POINT('Ctrl Pts',(-16.9905607104441,17.1806625191931,
18.9050252127084));
#210104=CARTESIAN_POINT('Ctrl Pts',(-19.4975018926199,16.6460602940324,
19.0322010193898));
#210105=CARTESIAN_POINT('Ctrl Pts',(-21.3039774764415,18.4646310475516,
19.1593768260712));
#210106=CARTESIAN_POINT('Ctrl Pts',(-20.7526582367037,20.9679489966759,
19.2865526327527));
#210107=CARTESIAN_POINT('Ctrl Pts',(-18.3493453563032,21.8593752771558,
19.4137284394341));
#210108=CARTESIAN_POINT('Ctrl Pts',(-16.2989292381897,20.3210816421169,
19.5409042461156));
#210109=CARTESIAN_POINT('Ctrl Pts',(-16.4825394044677,17.7643569525393,
19.668080052797));
#210110=CARTESIAN_POINT('Ctrl Pts',(-18.7317249296591,16.5348375614239,
19.7952558594784));
#210111=CARTESIAN_POINT('Ctrl Pts',(-20.9829976831335,17.760530930567,19.9224316661598));
#210112=CARTESIAN_POINT('Ctrl Pts',(-21.1709546654166,20.31693998334,20.0496074728413));
#210113=CARTESIAN_POINT('Ctrl Pts',(-19.1231569686169,21.8587170911293,
20.1767832795227));
#210114=CARTESIAN_POINT('Ctrl Pts',(-16.7183319609261,20.9713793612995,
20.3039590862042));
#210115=CARTESIAN_POINT('Ctrl Pts',(-16.1627571685425,18.4690004055044,
20.4311348928856));
#210116=CARTESIAN_POINT('Ctrl Pts',(-17.9661382852434,16.6473646938877,
20.558310699567));
#210117=CARTESIAN_POINT('Ctrl Pts',(-20.4739844799035,17.1776962596402,
20.6854865062485));
#210118=CARTESIAN_POINT('Ctrl Pts',(-21.3855036545633,19.573475146687,20.8126623129299));
#210119=CARTESIAN_POINT('Ctrl Pts',(-19.8644313620253,21.6366721694472,
20.9398381196113));
#210120=CARTESIAN_POINT('Ctrl Pts',(-17.3062612225653,21.4745299209001,
21.0670139262928));
#210121=CARTESIAN_POINT('Ctrl Pts',(-16.0579474672366,19.2356153818981,
21.1941897329742));
#210122=CARTESIAN_POINT('Ctrl Pts',(-17.2647560855632,16.9743568582036,
21.3213655396557));
#210123=CARTESIAN_POINT('Ctrl Pts',(-19.8194850045369,16.7646188200965,
21.448541346337));
#210124=CARTESIAN_POINT('Ctrl Pts',(-21.3783870556072,18.8001718981978,
21.5757171530185));
#210125=CARTESIAN_POINT('Ctrl Pts',(-20.5111534744378,21.210919657188,21.7028929596999));
#210126=CARTESIAN_POINT('Ctrl Pts',(-18.013644503055,21.7901978133332,21.8300687663814));
#210127=CARTESIAN_POINT('Ctrl Pts',(-16.1763704623236,19.996267194463,21.9572632304172));
#210128=CARTESIAN_POINT('Ctrl Pts',(-16.5172189858702,18.3298181259339,
22.0420657588926));
#210129=CARTESIAN_POINT('Ctrl Pts',(-17.0028273589161,17.7531907778071,
22.0844763518074));
#210130=CARTESIAN_POINT('Ctrl Pts',(-19.2802416061914,17.1696268270448,
-0.257964187031692));
#210131=CARTESIAN_POINT('Ctrl Pts',(-19.9599075838988,17.3514955026281,
-0.215572251471214));
#210132=CARTESIAN_POINT('Ctrl Pts',(-21.1114421336233,18.4445263035272,
-0.130788380350257));
#210133=CARTESIAN_POINT('Ctrl Pts',(-20.664716890137,20.7997959707902,-0.00361257366882362));
#210134=CARTESIAN_POINT('Ctrl Pts',(-18.4433885124361,21.6921206442111,
0.123563233012611));
#210135=CARTESIAN_POINT('Ctrl Pts',(-16.4903436032298,20.310803390867,0.250739039694045));
#210136=CARTESIAN_POINT('Ctrl Pts',(-16.5948543226392,17.9191325598114,
0.37791484637548));
#210137=CARTESIAN_POINT('Ctrl Pts',(-18.6623441835338,16.7133702016597,
0.505090653056915));
#210138=CARTESIAN_POINT('Ctrl Pts',(-20.7953425359789,17.7986649093718,
0.632266459738347));
#210139=CARTESIAN_POINT('Ctrl Pts',(-21.0373070659623,20.1798778964501,
0.759442266419783));
#210140=CARTESIAN_POINT('Ctrl Pts',(-19.1660680424989,21.6721077326961,
0.886618073101216));
#210141=CARTESIAN_POINT('Ctrl Pts',(-16.8984657270469,20.9064747389806,
1.01379387978265));
#210142=CARTESIAN_POINT('Ctrl Pts',(-16.3148354086541,18.5853225629306,
1.14096968646408));
#210143=CARTESIAN_POINT('Ctrl Pts',(-17.9506471564477,16.8382042717466,
1.26814549314552));
#210144=CARTESIAN_POINT('Ctrl Pts',(-20.305132000971,17.2679716947772,1.39532129982695));
#210145=CARTESIAN_POINT('Ctrl Pts',(-21.2182030940675,19.4803506713964,
1.52249710650838));
#210146=CARTESIAN_POINT('Ctrl Pts',(-19.8521708189713,21.445615214303,1.64967291318982));
#210147=CARTESIAN_POINT('Ctrl Pts',(-17.4602868502336,21.3607599853939,
1.77684871987125));
#210148=CARTESIAN_POINT('Ctrl Pts',(-16.236955313264,19.3036328845313,1.90402452655269));
#210149=CARTESIAN_POINT('Ctrl Pts',(-17.3045074623036,17.1615211285584,
2.03120033323412));
#210150=CARTESIAN_POINT('Ctrl Pts',(-19.6835302021449,16.8996788935686,
2.15837613991555));
#210151=CARTESIAN_POINT('Ctrl Pts',(-21.1914179617914,18.758330388868,2.28555194659699));
#210152=CARTESIAN_POINT('Ctrl Pts',(-20.444777242296,21.0322781192214,2.41272775327842));
#210153=CARTESIAN_POINT('Ctrl Pts',(-18.1286045981342,21.6353162358223,
2.53990355995986));
#210154=CARTESIAN_POINT('Ctrl Pts',(-16.3678446537097,20.0141946660428,
2.66707936664131));
#210155=CARTESIAN_POINT('Ctrl Pts',(-16.7778853826632,17.6561918472671,
2.79425517332272));
#210156=CARTESIAN_POINT('Ctrl Pts',(-18.9825398611346,16.7246290036402,
2.92143098000418));
#210157=CARTESIAN_POINT('Ctrl Pts',(-20.9591744440326,18.0741572289896,
3.04860678668559));
#210158=CARTESIAN_POINT('Ctrl Pts',(-20.8943495839686,20.4666681355921,
3.17578259336703));
#210159=CARTESIAN_POINT('Ctrl Pts',(-18.8475380672715,21.7071814637211,
3.30295840004846));
#210160=CARTESIAN_POINT('Ctrl Pts',(-16.696562420695,20.6576032291843,3.4301342067299));
#210161=CARTESIAN_POINT('Ctrl Pts',(-16.4148092955578,18.2808563182951,
3.55731001341133));
#210162=CARTESIAN_POINT('Ctrl Pts',(-18.2607696965035,16.7574585040896,
3.68448582009278));
#210163=CARTESIAN_POINT('Ctrl Pts',(-20.5408895289395,17.4850327284497,
3.8116616267742));
#210164=CARTESIAN_POINT('Ctrl Pts',(-21.1633003667766,19.7960747988325,
3.93883743345564));
#210165=CARTESIAN_POINT('Ctrl Pts',(-19.5569788974863,21.5703470551314,
4.06601324013707));
#210166=CARTESIAN_POINT('Ctrl Pts',(-17.1956253695811,21.1800648259367,
4.19318904681852));
#210167=CARTESIAN_POINT('Ctrl Pts',(-16.2456350827884,18.9832878328934,
4.32036485349995));
#210168=CARTESIAN_POINT('Ctrl Pts',(-17.5785651621917,16.9954226197583,
4.44754066018137));
#210169=CARTESIAN_POINT('Ctrl Pts',(-19.9715349909106,17.0402121387546,
4.57471646686281));
#210170=CARTESIAN_POINT('Ctrl Pts',(-21.2291432755529,19.0765647861535,
4.70189227354424));
#210171=CARTESIAN_POINT('Ctrl Pts',(-20.1976124709327,21.2362533982663,
4.82906808022569));
#210172=CARTESIAN_POINT('Ctrl Pts',(-17.8233080662669,21.5378977188721,
4.95624388690712));
#210173=CARTESIAN_POINT('Ctrl Pts',(-16.2845069868849,19.7047578059733,
5.08341969358855));
#210174=CARTESIAN_POINT('Ctrl Pts',(-16.9929637143536,17.4186257521595,
5.21059550026999));
#210175=CARTESIAN_POINT('Ctrl Pts',(-19.298713173004,16.7768858234474,5.33777130695141));
#210176=CARTESIAN_POINT('Ctrl Pts',(-21.0863733454756,18.368294573558,5.46494711363286));
#210177=CARTESIAN_POINT('Ctrl Pts',(-20.7158769782294,20.7328332482315,
5.59212292031427));
#210178=CARTESIAN_POINT('Ctrl Pts',(-18.5271314926159,21.7011843732767,
5.71929872699574));
#210179=CARTESIAN_POINT('Ctrl Pts',(-16.5281750228197,20.3849458941136,
5.84647453367714));
#210180=CARTESIAN_POINT('Ctrl Pts',(-16.5529260606478,17.9916849204009,
5.9736503403586));
#210181=CARTESIAN_POINT('Ctrl Pts',(-18.5786770651157,16.7170698529915,
6.10082614704002));
#210182=CARTESIAN_POINT('Ctrl Pts',(-20.7469272219113,17.7304809047003,
6.22800195372147));
#210183=CARTESIAN_POINT('Ctrl Pts',(-21.0684415889569,20.1021763349681,
6.35517776040288));
#210184=CARTESIAN_POINT('Ctrl Pts',(-19.2482506899202,21.6562727905442,
6.48235356708434));
#210185=CARTESIAN_POINT('Ctrl Pts',(-16.9562667008792,20.9669832315418,
6.60952937376576));
#210186=CARTESIAN_POINT('Ctrl Pts',(-16.2952426752091,18.6666880462109,
6.7367051804472));
#210187=CARTESIAN_POINT('Ctrl Pts',(-17.8716271286841,16.8657652946716,
6.86388098712864));
#210188=CARTESIAN_POINT('Ctrl Pts',(-20.2391851666945,17.2164498235889,
6.99105679381006));
#210189=CARTESIAN_POINT('Ctrl Pts',(-21.2258292365902,19.397010343618,7.11823260049151));
#210190=CARTESIAN_POINT('Ctrl Pts',(-19.9263746422792,21.4069179184816,
7.24540840717293));
#210191=CARTESIAN_POINT('Ctrl Pts',(-17.5329903207938,21.4022070971754,
7.37258421385437));
#210192=CARTESIAN_POINT('Ctrl Pts',(-16.2414578369124,19.3871997658614,
7.49976002053581));
#210193=CARTESIAN_POINT('Ctrl Pts',(-17.2366780830498,17.2105400855604,
7.62693582721722));
#210194=CARTESIAN_POINT('Ctrl Pts',(-19.6055982537098,16.8691782142126,
7.75411163389868));
#210195=CARTESIAN_POINT('Ctrl Pts',(-21.1748811240797,18.6762924814722,
7.88128744058011));
#210196=CARTESIAN_POINT('Ctrl Pts',(-20.5048070612748,20.9739677092896,
8.00846324726155));
#210197=CARTESIAN_POINT('Ctrl Pts',(-18.2101274284319,21.6542294859505,
8.13563905394297));
#210198=CARTESIAN_POINT('Ctrl Pts',(-16.3960683648039,20.0929798531758,
8.26281486062441));
#210199=CARTESIAN_POINT('Ctrl Pts',(-16.7269164680658,17.7225684469559,
8.38999066730585));
#210200=CARTESIAN_POINT('Ctrl Pts',(-18.899139138224,16.717700608173,8.51716647398728));
#210201=CARTESIAN_POINT('Ctrl Pts',(-20.9198568987526,18.0002802097783,
8.64434228066872));
#210202=CARTESIAN_POINT('Ctrl Pts',(-20.9351866242553,20.3936200731671,
8.77151808735015));
#210203=CARTESIAN_POINT('Ctrl Pts',(-18.9310642430538,21.7019794211049,
8.89869389403158));
#210204=CARTESIAN_POINT('Ctrl Pts',(-16.7461476500366,20.7250197577984,
9.02586970071301));
#210205=CARTESIAN_POINT('Ctrl Pts',(-16.3849622080794,18.3590409373758,
9.15304550739446));
#210206=CARTESIAN_POINT('Ctrl Pts',(-18.1788731424809,16.774681678368,9.28022131407588));
#210207=CARTESIAN_POINT('Ctrl Pts',(-20.4820785135977,17.4254932644886,
9.40739712075733));
#210208=CARTESIAN_POINT('Ctrl Pts',(-21.1815303464774,19.7143964593946,
9.53457292743875));
#210209=CARTESIAN_POINT('Ctrl Pts',(-19.6355249973296,21.5414646471141,
9.66174873412019));
#210210=CARTESIAN_POINT('Ctrl Pts',(-17.2624264180838,21.2304761660553,
9.78892454080163));
#210211=CARTESIAN_POINT('Ctrl Pts',(-16.2394052640888,19.0667436454676,
9.91610034748306));
#210212=CARTESIAN_POINT('Ctrl Pts',(-17.5050199482811,17.0353573766044,
10.0432761541645));
#210213=CARTESIAN_POINT('Ctrl Pts',(-19.8981475508207,16.9999881790961,
10.1704519608459));
#210214=CARTESIAN_POINT('Ctrl Pts',(-21.2232420306283,18.9930850963969,
10.2976277675273));
#210215=CARTESIAN_POINT('Ctrl Pts',(-20.264611447119,21.1861054124292,10.4248035742088));
#210216=CARTESIAN_POINT('Ctrl Pts',(-17.9017398613385,21.5670891014251,
10.5519793808902));
#210217=CARTESIAN_POINT('Ctrl Pts',(-16.30241529689,19.7865072752454,10.6791551875716));
#210218=CARTESIAN_POINT('Ctrl Pts',(-16.9339187763774,17.477933244038,10.8063309942531));
#210219=CARTESIAN_POINT('Ctrl Pts',(-19.2168850528976,16.7593403951717,
10.9335068009345));
#210220=CARTESIAN_POINT('Ctrl Pts',(-21.0568342646105,18.289993066579,11.0606826076159));
#210221=CARTESIAN_POINT('Ctrl Pts',(-20.7657272098974,20.6656124352628,
11.1878584142974));
#210222=CARTESIAN_POINT('Ctrl Pts',(-18.6106365433157,21.7067151780229,
11.3150342209788));
#210223=CARTESIAN_POINT('Ctrl Pts',(-16.5687241914422,20.4581541465005,
11.4422100276602));
#210224=CARTESIAN_POINT('Ctrl Pts',(-16.5133180017472,18.0654065926801,
11.5693858343417));
#210225=CARTESIAN_POINT('Ctrl Pts',(-18.4952497143798,16.7236698865299,
11.6965616410231));
#210226=CARTESIAN_POINT('Ctrl Pts',(-20.696219995555,17.6639041783707,11.8237374477046));
#210227=CARTESIAN_POINT('Ctrl Pts',(-21.0969752199166,20.0235028629602,
11.950913254386));
#210228=CARTESIAN_POINT('Ctrl Pts',(-19.3298473427874,21.6376806003988,
12.0780890610674));
#210229=CARTESIAN_POINT('Ctrl Pts',(-17.0160665111076,21.0255295037559,
12.2052648677489));
#210230=CARTESIAN_POINT('Ctrl Pts',(-16.278383028509,18.7486602098194,12.3324406744303));
#210231=CARTESIAN_POINT('Ctrl Pts',(-17.7935757044751,16.8959589773299,
12.4596164811117));
#210232=CARTESIAN_POINT('Ctrl Pts',(-20.1715493022707,17.1671641954894,
12.5867922877931));
#210233=CARTESIAN_POINT('Ctrl Pts',(-21.2306606396052,19.3134619095308,
12.7139680944746));
#210234=CARTESIAN_POINT('Ctrl Pts',(-19.9992408003375,21.365757181081,12.841143901156));
#210235=CARTESIAN_POINT('Ctrl Pts',(-17.6070410564606,21.4411964783031,
12.9683197078375));
#210236=CARTESIAN_POINT('Ctrl Pts',(-16.2487561963206,19.4705689282866,
13.0954955145189));
#210237=CARTESIAN_POINT('Ctrl Pts',(-17.1705282744295,17.2618029972318,
13.2226713212003));
#210238=CARTESIAN_POINT('Ctrl Pts',(-19.52668862075,16.8413043354067,13.3498471278818));
#210239=CARTESIAN_POINT('Ctrl Pts',(-21.1556063573368,18.5948543659455,
13.4770229345632));
#210240=CARTESIAN_POINT('Ctrl Pts',(-20.5628505629085,20.9136797734184,
13.6041987412446));
#210241=CARTESIAN_POINT('Ctrl Pts',(-18.2922378882792,21.670402169005,13.7313745479261));
#210242=CARTESIAN_POINT('Ctrl Pts',(-16.4269145323048,20.1707757222437,
13.8585503546075));
#210243=CARTESIAN_POINT('Ctrl Pts',(-16.6781988990673,17.7906146207234,
13.9857261612889));
#210244=CARTESIAN_POINT('Ctrl Pts',(-18.8155531785289,16.7135689456302,
14.1129019679704));
#210245=CARTESIAN_POINT('Ctrl Pts',(-20.8780874784513,17.9277612548684,
14.2400777746518));
#210246=CARTESIAN_POINT('Ctrl Pts',(-20.9735545939718,20.3192454659859,
14.3672535813332));
#210247=CARTESIAN_POINT('Ctrl Pts',(-19.0143693719578,21.6939832475324,
14.4944293880147));
#210248=CARTESIAN_POINT('Ctrl Pts',(-16.7979626528582,20.7907380107889,
14.6216051946961));
#210249=CARTESIAN_POINT('Ctrl Pts',(-16.3577500357315,18.4381811987453,
14.7487810013775));
#210250=CARTESIAN_POINT('Ctrl Pts',(-18.0975992741149,16.7946376703086,
14.875956808059));
#210251=CARTESIAN_POINT('Ctrl Pts',(-20.4213066790141,17.3679566030033,
15.0031326147404));
#210252=CARTESIAN_POINT('Ctrl Pts',(-21.1970149319813,19.6321534602683,
15.1303084214219));
#210253=CARTESIAN_POINT('Ctrl Pts',(-19.713059856803,21.5099681574688,15.2574842281033));
#210254=CARTESIAN_POINT('Ctrl Pts',(-17.3308781303159,21.2786222602481,
15.3846600347847));
#210255=CARTESIAN_POINT('Ctrl Pts',(-16.2359736316991,19.1503612703603,
15.5118358414661));
#210256=CARTESIAN_POINT('Ctrl Pts',(-17.432853280996,17.0777325512529,15.6390116481476));
#210257=CARTESIAN_POINT('Ctrl Pts',(-19.8234542867059,16.9622443108606,
15.766187454829));
#210258=CARTESIAN_POINT('Ctrl Pts',(-21.2145486035221,18.9098498417347,
15.8933632615105));
#210259=CARTESIAN_POINT('Ctrl Pts',(-20.3298935368166,21.1337419513304,
16.0205390681919));
#210260=CARTESIAN_POINT('Ctrl Pts',(-17.9811052024058,21.5936376594049,
16.1477148748733));
#210261=CARTESIAN_POINT('Ctrl Pts',(-16.3230511148663,19.8676111981466,
16.2748906815548));
#210262=CARTESIAN_POINT('Ctrl Pts',(-16.8768929890729,17.5391847164761,
16.4020664882362));
#210263=CARTESIAN_POINT('Ctrl Pts',(-19.1345152807445,16.7445449928796,
16.5292422949176));
#210264=CARTESIAN_POINT('Ctrl Pts',(-21.0246896611148,18.2127246528537,
16.656418101599));
#210265=CARTESIAN_POINT('Ctrl Pts',(-20.8132984536472,20.5967599838785,
16.7835939082805));
#210266=CARTESIAN_POINT('Ctrl Pts',(-18.6942799707749,21.7094465396596,
16.9107697149619));
#210267=CARTESIAN_POINT('Ctrl Pts',(-16.6117021494137,20.5299634663839,
17.0379455216434));
#210268=CARTESIAN_POINT('Ctrl Pts',(-16.4762008813049,18.1404132768064,
17.1651213283248));
#210269=CARTESIAN_POINT('Ctrl Pts',(-18.4120901697813,16.7330599576527,
17.2922971350062));
#210270=CARTESIAN_POINT('Ctrl Pts',(-20.6433117475059,17.5990628290491,
17.4194729416877));
#210271=CARTESIAN_POINT('Ctrl Pts',(-21.1228583021457,19.9439180066875,
17.5466487483691));
#210272=CARTESIAN_POINT('Ctrl Pts',(-19.4107756338348,21.6163664032144,
17.6738245550505));
#210273=CARTESIAN_POINT('Ctrl Pts',(-17.0777933269134,21.0820404186637,
17.801000361732));
#210274=CARTESIAN_POINT('Ctrl Pts',(-16.2642778467699,18.8311509798632,
17.9281761684134));
#210275=CARTESIAN_POINT('Ctrl Pts',(-17.7165791539697,16.9287494409323,
18.0553519750948));
#210276=CARTESIAN_POINT('Ctrl Pts',(-20.1023009391443,17.1201711375333,
18.1825277817763));
#210277=CARTESIAN_POINT('Ctrl Pts',(-21.2326915389853,19.2297985439103,
18.3097035884577));
#210278=CARTESIAN_POINT('Ctrl Pts',(-20.0706877380999,21.3221794531393,
18.4368793951392));
#210279=CARTESIAN_POINT('Ctrl Pts',(-17.6823559016955,21.4776842484555,
18.5640552018205));
#210280=CARTESIAN_POINT('Ctrl Pts',(-16.2588422531106,19.5536469325526,
18.691231008502));
#210281=CARTESIAN_POINT('Ctrl Pts',(-17.1061322116441,17.3152523222366,
18.8184068151834));
#210282=CARTESIAN_POINT('Ctrl Pts',(-19.4468898291958,16.8160885445611,
18.9455826218649));
#210283=CARTESIAN_POINT('Ctrl Pts',(-21.1336152752557,18.5141073790766,
19.0727584285463));
#210284=CARTESIAN_POINT('Ctrl Pts',(-20.6188426434545,20.8514819454316,
19.1999342352277));
#210285=CARTESIAN_POINT('Ctrl Pts',(-18.3748438723008,21.6838161347437,
19.3271100419092));
#210286=CARTESIAN_POINT('Ctrl Pts',(-16.4603485575527,20.2474950236424,
19.4542858485906));
#210287=CARTESIAN_POINT('Ctrl Pts',(-16.6317873206282,17.8602540162898,
19.5814616552721));
#210288=CARTESIAN_POINT('Ctrl Pts',(-18.7318757426506,16.712238697405,19.7086374619535));
#210289=CARTESIAN_POINT('Ctrl Pts',(-20.833913031897,17.8566816189236,19.8358132686349));
#210290=CARTESIAN_POINT('Ctrl Pts',(-21.0094104632606,20.243627912838,19.9629890753163));
#210291=CARTESIAN_POINT('Ctrl Pts',(-19.0973599963134,21.6832015794576,
20.0901648819978));
#210292=CARTESIAN_POINT('Ctrl Pts',(-16.8519493358426,20.8546849133278,
20.2173406886792));
#210293=CARTESIAN_POINT('Ctrl Pts',(-16.3332032493219,18.5181870950206,
20.3445164953606));
#210294=CARTESIAN_POINT('Ctrl Pts',(-18.0170393585529,16.817306476565,20.4716923020421));
#210295=CARTESIAN_POINT('Ctrl Pts',(-20.3586419958767,17.3124826941761,
20.5988681087235));
#210296=CARTESIAN_POINT('Ctrl Pts',(-21.2097371339674,19.5494468956883,
20.726043915405));
#210297=CARTESIAN_POINT('Ctrl Pts',(-19.7894957733326,21.4758758768998,
20.8532197220864));
#210298=CARTESIAN_POINT('Ctrl Pts',(-17.4009051340672,21.3244819367018,
20.9803955287679));
#210299=CARTESIAN_POINT('Ctrl Pts',(-16.2353413176302,19.2339836436119,
21.1075713354492));
#210300=CARTESIAN_POINT('Ctrl Pts',(-17.3621513466646,17.1226225346138,
21.2347471421307));
#210301=CARTESIAN_POINT('Ctrl Pts',(-19.7475288817995,16.9267879000082,
21.3619229488121));
#210302=CARTESIAN_POINT('Ctrl Pts',(-21.2030922899096,18.82740543638,21.4890987554935));
#210303=CARTESIAN_POINT('Ctrl Pts',(-20.3933470809866,21.078346232667,21.616274562175));
#210304=CARTESIAN_POINT('Ctrl Pts',(-18.0613964188678,21.6192244017756,
21.7434503688564));
#210305=CARTESIAN_POINT('Ctrl Pts',(-16.3459141263638,19.9442123227787,
21.8706448328923));
#210306=CARTESIAN_POINT('Ctrl Pts',(-16.6641680142473,18.3882311218014,
21.9554473613676));
#210307=CARTESIAN_POINT('Ctrl Pts',(-17.1175857116532,17.849828040304,21.9978579542825));
#210308=CARTESIAN_POINT('Ctrl Pts',(-19.3957372685685,16.7380050975816,
-1.23165366794353E-15));
#210309=CARTESIAN_POINT('Ctrl Pts',(-19.4773890628972,16.7675693190178,
4.67785589882032E-15));
#210310=CARTESIAN_POINT('Ctrl Pts',(-19.5571491449816,16.8015339789003,
1.41562167189676E-14));
#210311=CARTESIAN_POINT('Ctrl Pts',(-19.6348154881074,16.8395812463466,
1.43895312332276E-14));
#210312=CARTESIAN_POINT('Ctrl Pts',(-19.7143271339378,16.8785324925655,
1.46283891513207E-14));
#210313=CARTESIAN_POINT('Ctrl Pts',(-19.7916450873999,16.9217633018164,
1.59364397924074E-15));
#210314=CARTESIAN_POINT('Ctrl Pts',(-19.8665231354208,16.9689790854395,
1.51961776495568E-15));
#210315=CARTESIAN_POINT('Ctrl Pts',(-19.93658856029,17.0131601775957,1.45034942406773E-15));
#210316=CARTESIAN_POINT('Ctrl Pts',(-20.0045177778054,17.0608314259457,
4.40057979472968E-15));
#210317=CARTESIAN_POINT('Ctrl Pts',(-20.0700782293505,17.1117789745462,
6.48786580015326E-15));
#210318=CARTESIAN_POINT('Ctrl Pts',(-20.0997466327889,17.1348345269478,
7.70028889287582E-15));
#210319=CARTESIAN_POINT('Ctrl Pts',(-20.1289294943527,17.1585613303937,
2.175758139592E-14));
#210320=CARTESIAN_POINT('Ctrl Pts',(-20.1576028725502,17.1829408480985,
1.05748743095546E-14));
#210321=CARTESIAN_POINT('Ctrl Pts',(-20.1753080913464,17.197994696729,3.78565993772445E-15));
#210322=CARTESIAN_POINT('Ctrl Pts',(-20.192819023282,17.213297426603,-2.39744414414718E-14));
#210323=CARTESIAN_POINT('Ctrl Pts',(-20.2101297182957,17.228844786453,-1.88668525247238E-14));
#210324=CARTESIAN_POINT('Ctrl Pts',(-20.2222917522923,17.2397679480536,
-1.53146598863056E-14));
#210325=CARTESIAN_POINT('Ctrl Pts',(-20.2343567224894,17.2508136607941,
-1.04410141243044E-14));
#210326=CARTESIAN_POINT('Ctrl Pts',(-20.2463056670645,17.2619643610397,
-1.12895803816571E-14));
#210327=CARTESIAN_POINT('Ctrl Pts',(-20.3097374450941,17.3211586052181,
-1.46324699270345E-14));
#210328=CARTESIAN_POINT('Ctrl Pts',(-20.3700068842138,17.3834001964164,
-1.31327203746279E-14));
#210329=CARTESIAN_POINT('Ctrl Pts',(-20.4268834249918,17.4484109388489,
-3.60822483003176E-16));
#210330=CARTESIAN_POINT('Ctrl Pts',(-20.4830375676461,17.5125959693496,
1.22488574722256E-14));
#210331=CARTESIAN_POINT('Ctrl Pts',(-20.5358849034917,17.5794810921972,
-4.53135006405206E-15));
#210332=CARTESIAN_POINT('Ctrl Pts',(-20.5851610289898,17.6488247163834,
-5.20417042793042E-15));
#210333=CARTESIAN_POINT('Ctrl Pts',(-20.630598257404,17.712766068496,-5.82457416800118E-15));
#210334=CARTESIAN_POINT('Ctrl Pts',(-20.6729989034477,17.7787984983208,
-1.74365969497394E-14));
#210335=CARTESIAN_POINT('Ctrl Pts',(-20.7121179763249,17.8467438133767,
5.55111512312578E-16));
#210336=CARTESIAN_POINT('Ctrl Pts',(-20.7284900279032,17.8751801775537,
7.98301933950798E-15));
#210337=CARTESIAN_POINT('Ctrl Pts',(-20.7442868194365,17.9039516828061,
-1.01106350429347E-15));
#210338=CARTESIAN_POINT('Ctrl Pts',(-20.7594882783128,17.9330455001009,
-1.22402088464924E-14));
#210339=CARTESIAN_POINT('Ctrl Pts',(-20.7693449710067,17.9519100590029,
-1.96477426282344E-14));
#210340=CARTESIAN_POINT('Ctrl Pts',(-20.7789513429732,17.970910128766,-2.31450257561518E-14));
#210341=CARTESIAN_POINT('Ctrl Pts',(-20.7883016221878,17.9900422154472,
-2.25652829755063E-14));
#210342=CARTESIAN_POINT('Ctrl Pts',(-20.7942275728048,18.0021676074567,
-2.21856505814976E-14));
#210343=CARTESIAN_POINT('Ctrl Pts',(-20.8000468301417,18.0143382523374,
8.10549747755472E-16));
#210344=CARTESIAN_POINT('Ctrl Pts',(-20.8057567255896,18.0265495880407,
7.07767178198537E-16));
#210345=CARTESIAN_POINT('Ctrl Pts',(-20.8408822594586,18.1016699978184,
4.51885638151754E-16));
#210346=CARTESIAN_POINT('Ctrl Pts',(-20.8718943559605,18.1783721483409,
2.2231995317661E-14));
#210347=CARTESIAN_POINT('Ctrl Pts',(-20.8985462175416,18.2564274689474,
7.60502771868232E-15));
#210348=CARTESIAN_POINT('Ctrl Pts',(-20.9251980791227,18.3344827895539,
-7.47990687795419E-15));
#210349=CARTESIAN_POINT('Ctrl Pts',(-20.9474901778909,18.4138920100306,
-4.35017343927013E-16));
#210350=CARTESIAN_POINT('Ctrl Pts',(-20.9651214076632,18.4944358221201,
7.68829444552921E-15));
#210351=CARTESIAN_POINT('Ctrl Pts',(-20.9829513884047,18.5758875777238,
1.55637816228134E-14));
#210352=CARTESIAN_POINT('Ctrl Pts',(-20.9960140913518,18.658500875996,-1.23111829755394E-14));
#210353=CARTESIAN_POINT('Ctrl Pts',(-21.0043852377911,18.7418839028421,
-4.82947015711943E-15));
#210354=CARTESIAN_POINT('Ctrl Pts',(-21.0073021823584,18.7709389037228,
-2.22245071022286E-15));
#210355=CARTESIAN_POINT('Ctrl Pts',(-21.0096490356195,18.8000872405028,
-2.55476121086874E-15));
#210356=CARTESIAN_POINT('Ctrl Pts',(-21.0114276099518,18.8293118127823,
-6.0507154842071E-15));
#210357=CARTESIAN_POINT('Ctrl Pts',(-21.0124180861882,18.8455867830405,
-7.99758920671491E-15));
#210358=CARTESIAN_POINT('Ctrl Pts',(-21.0132324466491,18.8618898462714,
-1.03347261259021E-14));
#210359=CARTESIAN_POINT('Ctrl Pts',(-21.013870300486,18.8781994765334,-6.80011602582908E-15));
#210360=CARTESIAN_POINT('Ctrl Pts',(-21.0156561553971,18.9238629680941,
3.09603955107904E-15));
#210361=CARTESIAN_POINT('Ctrl Pts',(-21.0160589030046,18.9695495767969,
5.33176806238529E-15));
#210362=CARTESIAN_POINT('Ctrl Pts',(-21.0151046780771,19.0152032718637,
6.38378239159465E-16));
#210363=CARTESIAN_POINT('Ctrl Pts',(-21.0142961185617,19.0538877879554,
-3.3385509858536E-15));
#210364=CARTESIAN_POINT('Ctrl Pts',(-21.0125130883268,19.0925470962694,
-8.9035032026131E-15));
#210365=CARTESIAN_POINT('Ctrl Pts',(-21.0097683504117,19.1311426359222,
-5.19029264012261E-15));
#210366=CARTESIAN_POINT('Ctrl Pts',(-21.0039587339496,19.2128354202505,
2.59522987051867E-15));
#210367=CARTESIAN_POINT('Ctrl Pts',(-20.9938436162584,19.2942438410436,
1.41268828373383E-14));
#210368=CARTESIAN_POINT('Ctrl Pts',(-20.9795069236666,19.3749917573276,
-1.80411241501588E-15));
#210369=CARTESIAN_POINT('Ctrl Pts',(-20.9654095554307,19.4543917376819,
-1.746916940066E-14));
#210370=CARTESIAN_POINT('Ctrl Pts',(-20.9472298872572,19.5331539565604,
6.03445153792289E-16));
#210371=CARTESIAN_POINT('Ctrl Pts',(-20.9250049246707,19.6108953906273,
1.41553435639707E-15));
#210372=CARTESIAN_POINT('Ctrl Pts',(-20.9157258007255,19.6433531461612,
1.75458898185226E-15));
#210373=CARTESIAN_POINT('Ctrl Pts',(-20.9057410484994,19.6756325821161,
2.59523708429575E-15));
#210374=CARTESIAN_POINT('Ctrl Pts',(-20.8950514018658,19.7077039335531,
-4.55191440096314E-15));
#210375=CARTESIAN_POINT('Ctrl Pts',(-20.8895107318069,19.72432719368,-8.07758464467123E-15));
#210376=CARTESIAN_POINT('Ctrl Pts',(-20.8837798046829,19.7408965824585,
8.50160659820308E-15));
#210377=CARTESIAN_POINT('Ctrl Pts',(-20.8778666060763,19.757386588617,5.02375918642883E-15));
#210378=CARTESIAN_POINT('Ctrl Pts',(-20.8511334429462,19.83193676932,-1.06923181167905E-14));
#210379=CARTESIAN_POINT('Ctrl Pts',(-20.8206474027028,19.9049627949995,
-1.73353012963057E-14));
#210380=CARTESIAN_POINT('Ctrl Pts',(-20.7864673380873,19.9761054066943,
-1.81799020282369E-14));
#210381=CARTESIAN_POINT('Ctrl Pts',(-20.7601551358713,20.0308717977514,
-1.8830085271024E-14));
#210382=CARTESIAN_POINT('Ctrl Pts',(-20.7316529099465,20.0845216847886,
-2.44471155034467E-16));
#210383=CARTESIAN_POINT('Ctrl Pts',(-20.7009723060731,20.1368764894501,
6.55031584528842E-15));
#210384=CARTESIAN_POINT('Ctrl Pts',(-20.6917380360057,20.1526342759514,
8.31297483703845E-15));
#210385=CARTESIAN_POINT('Ctrl Pts',(-20.6823063437492,20.1682746386422,
7.82297213918542E-15));
#210386=CARTESIAN_POINT('Ctrl Pts',(-20.6726773354748,20.1837924272005,
-6.38378239159465E-15));
#210387=CARTESIAN_POINT('Ctrl Pts',(-20.6644524181989,20.1970474295393,
-1.86960947630402E-14));
#210388=CARTESIAN_POINT('Ctrl Pts',(-20.6560858012134,20.2102092325172,
1.07604636562338E-14));
#210389=CARTESIAN_POINT('Ctrl Pts',(-20.64758209464,20.2232683236723,1.09634523681734E-14));
#210390=CARTESIAN_POINT('Ctrl Pts',(-20.6064305700017,20.286464473114,1.11814633947155E-14));
#210391=CARTESIAN_POINT('Ctrl Pts',(-20.5620419244788,20.3473056726972,
5.47217430806986E-15));
#210392=CARTESIAN_POINT('Ctrl Pts',(-20.5144495335262,20.4054521925719,
8.52096171399808E-15));
#210393=CARTESIAN_POINT('Ctrl Pts',(-20.4703173116583,20.4593712133354,
1.21050310956189E-14));
#210394=CARTESIAN_POINT('Ctrl Pts',(-20.4234297145935,20.5109732585207,
-9.13198254776251E-15));
#210395=CARTESIAN_POINT('Ctrl Pts',(-20.3737907847676,20.5599542646918,
-6.32827124036339E-15));
#210396=CARTESIAN_POINT('Ctrl Pts',(-20.3682022242118,20.5654687534213,
-6.1941711563184E-15));
#210397=CARTESIAN_POINT('Ctrl Pts',(-20.3625787693224,20.5709499818026,
-2.24943731332233E-15));
#210398=CARTESIAN_POINT('Ctrl Pts',(-20.3569207886222,20.5763978007994,
2.27595720048157E-15));
#210399=CARTESIAN_POINT('Ctrl Pts',(20.3504145334569,20.5721720813046,0.00214189615582165));
#210400=CARTESIAN_POINT('Ctrl Pts',(20.8038322552136,20.0337689331937,0.0445524877679971));
#210401=CARTESIAN_POINT('Ctrl Pts',(21.1220877011301,18.4777891502142,0.12935501494065));
#210402=CARTESIAN_POINT('Ctrl Pts',(19.4066027174179,16.8027744939582,0.256549477673783));
#210403=CARTESIAN_POINT('Ctrl Pts',(17.0746532806956,17.3436542441791,0.383725284355217));
#210404=CARTESIAN_POINT('Ctrl Pts',(16.2649072910693,19.5945942026566,0.510901091036652));
#210405=CARTESIAN_POINT('Ctrl Pts',(17.7204711796095,21.4952124979738,0.638076897718085));
#210406=CARTESIAN_POINT('Ctrl Pts',(20.1058486786829,21.2993774626889,0.765252704399521));
#210407=CARTESIAN_POINT('Ctrl Pts',(21.2326588902647,19.1880164416469,0.892428511080953));
#210408=CARTESIAN_POINT('Ctrl Pts',(20.06709493847,17.0975178673283,1.01960431776238));
#210409=CARTESIAN_POINT('Ctrl Pts',(17.6785041641668,16.9461239968056,1.14678012444382));
#210410=CARTESIAN_POINT('Ctrl Pts',(16.2582626906796,18.8725530643131,1.27395593112525));
#210411=CARTESIAN_POINT('Ctrl Pts',(17.1093578952725,21.1095174457449,1.40113173780669));
#210412=CARTESIAN_POINT('Ctrl Pts',(19.4509606892502,21.6046936825495,1.52830754448812));
#210413=CARTESIAN_POINT('Ctrl Pts',(21.1347969163821,19.9038129555627,1.65548335116956));
#210414=CARTESIAN_POINT('Ctrl Pts',(20.6160507930577,17.5673149720866,1.78265915785099));
#210415=CARTESIAN_POINT('Ctrl Pts',(18.3706399789337,16.7387982516159,1.90983496453243));
#210416=CARTESIAN_POINT('Ctrl Pts',(16.4585893803026,18.1783720157104,2.03701077121386));
#210417=CARTESIAN_POINT('Ctrl Pts',(16.6340868238919,20.5653184744001,2.16418657789529));
#210418=CARTESIAN_POINT('Ctrl Pts',(18.7361242574646,21.709761474113,2.29136238457673));
#210419=CARTESIAN_POINT('Ctrl Pts',(20.8362128238147,20.5617460765933,2.41853819125816));
#210420=CARTESIAN_POINT('Ctrl Pts',(21.0076515986441,18.1745049051026,2.54571399793959));
#210421=CARTESIAN_POINT('Ctrl Pts',(19.0931561523786,16.7381836953926,2.67288980462103));
#210422=CARTESIAN_POINT('Ctrl Pts',(16.84915722705,17.5705179418497,2.80006561130246));
#210423=CARTESIAN_POINT('Ctrl Pts',(16.3343845598861,19.9078926688087,2.9272414179839));
#210424=CARTESIAN_POINT('Ctrl Pts',(18.021110121826,21.605911619971,3.05441722466534));
#210425=CARTESIAN_POINT('Ctrl Pts',(20.3618679001945,21.1067478080081,3.18159303134677));
#210426=CARTESIAN_POINT('Ctrl Pts',(21.2091579169385,18.8683530439058,3.3087688380282));
#210427=CARTESIAN_POINT('Ctrl Pts',(19.7856441705552,16.9443155958186,3.43594464470964));
#210428=CARTESIAN_POINT('Ctrl Pts',(17.3973121700664,17.0998204018171,3.56312045139108));
#210429=CARTESIAN_POINT('Ctrl Pts',(16.2353082893486,19.1922014547983,3.69029625807252));
#210430=CARTESIAN_POINT('Ctrl Pts',(17.36569896685,21.3018290061115,3.81747206475393));
#210431=CARTESIAN_POINT('Ctrl Pts',(19.7514209159292,21.4932507158639,3.94464787143538));
#210432=CARTESIAN_POINT('Ctrl Pts',(21.2037223229058,19.5908490462335,4.0718236781168));
#210433=CARTESIAN_POINT('Ctrl Pts',(20.390206786872,17.3399594527915,4.19899948479825));
#210434=CARTESIAN_POINT('Ctrl Pts',(18.0572243196692,16.8056334315311,4.32617529147968));
#210435=CARTESIAN_POINT('Ctrl Pts',(16.345141533734,18.4780819429591,4.45335109816112));
#210436=CARTESIAN_POINT('Ctrl Pts',(16.8246881213196,20.8229372816948,4.58052690484254));
#210437=CARTESIAN_POINT('Ctrl Pts',(19.0559098523345,21.6889402125877,4.70770271152398));
#210438=CARTESIAN_POINT('Ctrl Pts',(20.9917992738112,20.2815867967456,4.83487851820543));
#210439=CARTESIAN_POINT('Ctrl Pts',(20.8562979963933,17.8920364430003,4.96205432488685));
#210440=CARTESIAN_POINT('Ctrl Pts',(18.7737200319539,16.7125532886911,5.0892301315683));
#210441=CARTESIAN_POINT('Ctrl Pts',(16.6547014035,17.8252399209163,5.21640593824972));
#210442=CARTESIAN_POINT('Ctrl Pts',(16.4433101815092,20.2092754157301,5.34358174493117));
#210443=CARTESIAN_POINT('Ctrl Pts',(18.3334846917389,21.6774551765717,5.47075755161258));
#210444=CARTESIAN_POINT('Ctrl Pts',(20.5911071385146,20.8828153983818,5.59793335829403));
#210445=CARTESIAN_POINT('Ctrl Pts',(21.1449490507717,18.5543887567427,5.72510916497546));
#210446=CARTESIAN_POINT('Ctrl Pts',(19.48689484932,16.8283621769022,5.8522849716569));
#210447=CARTESIAN_POINT('Ctrl Pts',(17.1381063535418,17.2882579165725,5.97946077833833));
#210448=CARTESIAN_POINT('Ctrl Pts',(16.2534512260582,19.5121501789549,6.10663658501977));
#210449=CARTESIAN_POINT('Ctrl Pts',(17.6445456384458,21.4597558436343,6.2338123917012));
#210450=CARTESIAN_POINT('Ctrl Pts',(20.0351468083957,21.3442675953079,6.36098819838264));
#210451=CARTESIAN_POINT('Ctrl Pts',(21.2320265399213,19.271638733806,6.48816400506407));
#210452=CARTESIAN_POINT('Ctrl Pts',(20.137121966082,17.1433775977014,6.6153398117455));
#210453=CARTESIAN_POINT('Ctrl Pts',(17.7549400759333,16.9120316845865,6.74251561842694));
#210454=CARTESIAN_POINT('Ctrl Pts',(16.2709848988036,18.7898465107973,6.86969142510837));
#210455=CARTESIAN_POINT('Ctrl Pts',(17.0466932050637,21.0540435236181,6.99686723178981));
#210456=CARTESIAN_POINT('Ctrl Pts',(19.3704007696072,21.6273624957014,7.12404303847125));
#210457=CARTESIAN_POINT('Ctrl Pts',(21.1102501275226,19.9838188543493,7.25121884515266));
#210458=CARTESIAN_POINT('Ctrl Pts',(20.6700374801522,17.6312618806795,7.37839465183412));
#210459=CARTESIAN_POINT('Ctrl Pts',(18.4536306087803,16.7280165818807,7.50557045851553));
#210460=CARTESIAN_POINT('Ctrl Pts',(16.4944452521654,18.1027544578749,7.63274626519699));
#210461=CARTESIAN_POINT('Ctrl Pts',(16.5899123742445,20.494238833293,7.7599220718784));
#210462=CARTESIAN_POINT('Ctrl Pts',(18.6524468158679,21.7084312259493,7.88709787855985));
#210463=CARTESIAN_POINT('Ctrl Pts',(20.7898012421711,20.6313854768606,8.01427368524127));
#210464=CARTESIAN_POINT('Ctrl Pts',(21.0410856261976,18.2512242118175,8.14144949192272));
#210465=CARTESIAN_POINT('Ctrl Pts',(19.175762142071,16.7515976620282,8.26862529860414));
#210466=CARTESIAN_POINT('Ctrl Pts',(16.9051493114451,17.5083201096033,8.39580110528559));
#210467=CARTESIAN_POINT('Ctrl Pts',(16.3123934762929,19.827145676385,8.52297691196702));
#210468=CARTESIAN_POINT('Ctrl Pts',(17.9413113247901,21.580695827397,8.65015271864845));
#210469=CARTESIAN_POINT('Ctrl Pts',(20.2974718329846,21.1601971366828,8.77732852532987));
#210470=CARTESIAN_POINT('Ctrl Pts',(21.2192439744216,18.9514310538806,8.90450433201132));
#210471=CARTESIAN_POINT('Ctrl Pts',(19.8609590209642,16.9808033684772,9.03168013869275));
#210472=CARTESIAN_POINT('Ctrl Pts',(17.4687591127375,17.0562426708819,9.1588559453742));
#210473=CARTESIAN_POINT('Ctrl Pts',(16.2373391888682,19.1085380834297,9.28603175205562));
#210474=CARTESIAN_POINT('Ctrl Pts',(17.296450598966,21.2548359449271,9.41320755873706));
#210475=CARTESIAN_POINT('Ctrl Pts',(19.6744243601341,21.526041181719,9.54038336541849));
#210476=CARTESIAN_POINT('Ctrl Pts',(21.1896171401977,19.6733398219446,9.66755917209993));
#210477=CARTESIAN_POINT('Ctrl Pts',(20.4519336069186,17.3964703715816,9.79473497878135));
#210478=CARTESIAN_POINT('Ctrl Pts',(18.1381526162766,16.7843192328824,9.9219107854628));
#210479=CARTESIAN_POINT('Ctrl Pts',(16.3710246177412,18.3984970812188,10.0490865921442));
#210480=CARTESIAN_POINT('Ctrl Pts',(16.7717798696356,20.7580959279184,10.1762623988257));
#210481=CARTESIAN_POINT('Ctrl Pts',(18.9727503020227,21.6983302843557,10.3034382055071));
#210482=CARTESIAN_POINT('Ctrl Pts',(20.9546821508189,20.356593486025,10.4306140121885));
#210483=CARTESIAN_POINT('Ctrl Pts',(20.8992759573175,17.9638457678171,10.5577898188699));
#210484=CARTESIAN_POINT('Ctrl Pts',(18.8573634651597,16.7152846505156,10.6849656255514));
#210485=CARTESIAN_POINT('Ctrl Pts',(16.7022726505182,17.7563874648017,10.8121414322328));
#210486=CARTESIAN_POINT('Ctrl Pts',(16.411165575805,20.1320069966963,10.9393172389142));
#210487=CARTESIAN_POINT('Ctrl Pts',(18.2511149139269,21.6626597732632,11.0664930455957));
#210488=CARTESIAN_POINT('Ctrl Pts',(20.5340813472922,20.9440668750279,11.1936688522771));
#210489=CARTESIAN_POINT('Ctrl Pts',(21.1655848701657,18.635492685216,11.3208446589586));
#210490=CARTESIAN_POINT('Ctrl Pts',(19.5662601958398,16.854910736706,11.44802046564));
#210491=CARTESIAN_POINT('Ctrl Pts',(17.2033884477244,17.2358944518762,11.5751962723214));
#210492=CARTESIAN_POINT('Ctrl Pts',(16.2447577983548,19.4289149185742,11.7023720790029));
#210493=CARTESIAN_POINT('Ctrl Pts',(17.5698523691992,21.4220119728056,11.8295478856843));
#210494=CARTESIAN_POINT('Ctrl Pts',(19.9629801361526,21.3866427728676,11.9567236923657));
#210495=CARTESIAN_POINT('Ctrl Pts',(21.2285949072958,19.3552563644432,12.0838994990471));
#210496=CARTESIAN_POINT('Ctrl Pts',(20.2055736830169,17.191523695202,12.2110753057286));
#210497=CARTESIAN_POINT('Ctrl Pts',(17.8324749407335,16.8805351927773,12.33825111241));
#210498=CARTESIAN_POINT('Ctrl Pts',(16.2864694853713,18.7076035060207,12.4654269190915));
#210499=CARTESIAN_POINT('Ctrl Pts',(16.985921366305,20.9965068581799,12.5926027257729));
#210500=CARTESIAN_POINT('Ctrl Pts',(19.2891268956574,21.647318489013,12.7197785324543));
#210501=CARTESIAN_POINT('Ctrl Pts',(21.0830379533052,20.0629591211559,12.8469543391357));
#210502=CARTESIAN_POINT('Ctrl Pts',(20.7218524865336,17.6969801381849,12.9741301458172));
#210503=CARTESIAN_POINT('Ctrl Pts',(18.5369357434076,16.7200204077588,13.1013059524986));
#210504=CARTESIAN_POINT('Ctrl Pts',(16.5328132245178,18.0283798455839,13.2284817591801));
#210505=CARTESIAN_POINT('Ctrl Pts',(16.5481429510737,20.4217198734009,13.3556575658615));
#210506=CARTESIAN_POINT('Ctrl Pts',(18.5688608504302,21.7042995631227,13.4828333725429));
#210507=CARTESIAN_POINT('Ctrl Pts',(20.7410836698255,20.6994316553031,13.6100091792244));
#210508=CARTESIAN_POINT('Ctrl Pts',(21.0719317958176,18.3290200862303,13.7371849859058));
#210509=CARTESIAN_POINT('Ctrl Pts',(19.2578726075595,16.7677703461939,13.8643607925872));
#210510=CARTESIAN_POINT('Ctrl Pts',(16.9631928170665,17.4480321695901,13.9915365992687));
#210511=CARTESIAN_POINT('Ctrl Pts',(16.2931187082259,19.7457075552633,14.1187124059501));
#210512=CARTESIAN_POINT('Ctrl Pts',(17.862401686409,21.5528219466762,14.2458882126315));
#210513=CARTESIAN_POINT('Ctrl Pts',(20.2313220198197,21.211460051876,14.373064019313));
#210514=CARTESIAN_POINT('Ctrl Pts',(21.2265423343311,19.0348002220335,14.5002398259944));
#210515=CARTESIAN_POINT('Ctrl Pts',(19.9350097617186,17.0197927522835,14.6274156326758));
#210516=CARTESIAN_POINT('Ctrl Pts',(17.5416252758018,17.0150819306536,14.7545914393573));
#210517=CARTESIAN_POINT('Ctrl Pts',(16.2421705922151,19.0249896436024,14.8817672460387));
#210518=CARTESIAN_POINT('Ctrl Pts',(17.2288147298954,21.2055503134414,15.0089430527202));
#210519=CARTESIAN_POINT('Ctrl Pts',(19.5963729305628,21.5562348664518,15.1361188594016));
#210520=CARTESIAN_POINT('Ctrl Pts',(21.1727574923393,19.7553119911849,15.263294666083));
#210521=CARTESIAN_POINT('Ctrl Pts',(20.5117334212554,17.455016647818,15.3904704727644));
#210522=CARTESIAN_POINT('Ctrl Pts',(18.2197492747497,16.7657270414598,15.5176462794459));
#210523=CARTESIAN_POINT('Ctrl Pts',(16.3995582506614,18.3198236038058,15.6448220861273));
#210524=CARTESIAN_POINT('Ctrl Pts',(16.7210726397956,20.6915191970148,15.7719978928088));
#210525=CARTESIAN_POINT('Ctrl Pts',(18.8893229455551,21.7049303183475,15.8991736994902));
#210526=CARTESIAN_POINT('Ctrl Pts',(20.915074089197,20.4303151633691,16.0263495061716));
#210527=CARTESIAN_POINT('Ctrl Pts',(20.9398251287259,18.0370540252336,16.153525312853));
#210528=CARTESIAN_POINT('Ctrl Pts',(18.9408685215966,16.7208154556417,16.2807011195345));
#210529=CARTESIAN_POINT('Ctrl Pts',(16.7521228856109,17.6891666472147,16.4078769262159));
#210530=CARTESIAN_POINT('Ctrl Pts',(16.3816264929107,20.0537054843378,16.5350527328974));
#210531=CARTESIAN_POINT('Ctrl Pts',(18.1692867881987,21.6451143437821,16.6622285395788));
#210532=CARTESIAN_POINT('Ctrl Pts',(20.4750364052595,21.003374370981,16.7894043462602));
#210533=CARTESIAN_POINT('Ctrl Pts',(21.1834931814011,18.7172421601046,16.9165801529417));
#210534=CARTESIAN_POINT('Ctrl Pts',(19.6446919963,16.8841021212645,17.0437559596231));
#210535=CARTESIAN_POINT('Ctrl Pts',(17.2703874285137,17.1857464625939,17.1709317663045));
#210536=CARTESIAN_POINT('Ctrl Pts',(16.2388565530248,19.3454352230824,17.298107572986));
#210537=CARTESIAN_POINT('Ctrl Pts',(17.4964649240676,21.3817880103836,17.4252833796674));
#210538=CARTESIAN_POINT('Ctrl Pts',(19.8894349171892,21.4265775324573,17.5524591863489));
#210539=CARTESIAN_POINT('Ctrl Pts',(21.2223650881682,19.4387121827512,17.6796349930303));
#210540=CARTESIAN_POINT('Ctrl Pts',(20.272374736109,17.2419350387839,17.8068107997117));
#210541=CARTESIAN_POINT('Ctrl Pts',(17.9110210459732,16.8516527827758,17.9339866063932));
#210542=CARTESIAN_POINT('Ctrl Pts',(16.3046994663247,18.6259251609712,18.0611624130746));
#210543=CARTESIAN_POINT('Ctrl Pts',(16.9271103469226,20.9369673901283,18.188338219756));
#210544=CARTESIAN_POINT('Ctrl Pts',(19.2072303360084,21.6645416644746,18.3155140264374));
#210545=CARTESIAN_POINT('Ctrl Pts',(21.053190863776,20.1411437456081,18.4426898331189));
#210546=CARTESIAN_POINT('Ctrl Pts',(20.7714377192819,17.764396671431,18.5698656398003));
#210547=CARTESIAN_POINT('Ctrl Pts',(18.6204619249281,16.714818364785,18.6970414464817));
#210548=CARTESIAN_POINT('Ctrl Pts',(16.5736502676105,17.9553317781408,18.8242172531632));
#210549=CARTESIAN_POINT('Ctrl Pts',(16.5088254030919,20.347842849113,18.9513930598446));
#210550=CARTESIAN_POINT('Ctrl Pts',(18.4854601217909,21.6973711671813,19.078568866526));
#210551=CARTESIAN_POINT('Ctrl Pts',(20.6901147517246,20.7658082595486,19.2057446732075));
#210552=CARTESIAN_POINT('Ctrl Pts',(21.100155508854,18.4078052787827,19.3329204798889));
#210553=CARTESIAN_POINT('Ctrl Pts',(19.3393954434522,16.786683597609,19.4600962865703));
#210554=CARTESIAN_POINT('Ctrl Pts',(17.02322264018,17.3897217556752,19.5872720932518));
#210555=CARTESIAN_POINT('Ctrl Pts',(16.2765818693588,19.6636696421892,19.7144478999332));
#210556=CARTESIAN_POINT('Ctrl Pts',(17.7844697326546,21.5223212653023,19.8416237066147));
#210557=CARTESIAN_POINT('Ctrl Pts',(20.1634926358433,21.2604790121031,19.9687995132961));
#210558=CARTESIAN_POINT('Ctrl Pts',(21.231044858401,19.1183671093666,20.0959753199775));
#210559=CARTESIAN_POINT('Ctrl Pts',(20.0077132370737,17.0612398664333,20.2231511266589));
#210560=CARTESIAN_POINT('Ctrl Pts',(17.6158291045619,16.976384633048,20.3503269333404));
#210561=CARTESIAN_POINT('Ctrl Pts',(16.2497967346393,18.9416493085074,20.4775027400218));
#210562=CARTESIAN_POINT('Ctrl Pts',(17.1628678921721,21.1540284415978,20.6046785467032));
#210563=CARTESIAN_POINT('Ctrl Pts',(19.5173528955041,21.5837958860619,20.7318543533847));
#210564=CARTESIAN_POINT('Ctrl Pts',(21.1531647607153,19.8366774894172,20.8590301600661));
#210565=CARTESIAN_POINT('Ctrl Pts',(20.5695343937816,17.5155251277943,20.9862059667476));
#210566=CARTESIAN_POINT('Ctrl Pts',(18.301931936395,16.7498921279798,21.113381773429));
#210567=CARTESIAN_POINT('Ctrl Pts',(16.430692762331,18.2421219844588,21.2405575801104));
#210568=CARTESIAN_POINT('Ctrl Pts',(16.6726573424412,20.6233352795928,21.3677333867919));
#210569=CARTESIAN_POINT('Ctrl Pts',(18.8056557941431,21.7086298106478,21.4949091934733));
#210570=CARTESIAN_POINT('Ctrl Pts',(20.8731458549779,20.5028678015929,21.6220850001547));
#210571=CARTESIAN_POINT('Ctrl Pts',(20.9776565334948,18.111196073242,21.7492608068362));
#210572=CARTESIAN_POINT('Ctrl Pts',(19.0246114642159,16.7298799538284,21.8764366135176));
#210573=CARTESIAN_POINT('Ctrl Pts',(16.8032831853607,17.6222026293144,22.0036124201991));
#210574=CARTESIAN_POINT('Ctrl Pts',(16.3565572075883,19.9774759742341,22.1307882268804));
#210575=CARTESIAN_POINT('Ctrl Pts',(17.5080922618947,21.070504731278,22.2155720980014));
#210576=CARTESIAN_POINT('Ctrl Pts',(18.1877583250969,21.2523734297384,22.2579640335619));
#210577=CARTESIAN_POINT('Ctrl Pts',(20.4651728790455,20.6688093317616,-0.0844764937345476));
#210578=CARTESIAN_POINT('Ctrl Pts',(20.9507812712845,20.0921819204693,-0.042065902122372));
#210579=CARTESIAN_POINT('Ctrl Pts',(21.2916314586439,18.4257343942419,0.0427366250502814));
#210580=CARTESIAN_POINT('Ctrl Pts',(19.4543545616952,16.6318010405789,0.169931087783413));
#210581=CARTESIAN_POINT('Ctrl Pts',(16.9568469381246,17.2110808818736,0.297106894464847));
#210582=CARTESIAN_POINT('Ctrl Pts',(16.0896125331239,19.6218277093859,0.424282701146282));
#210583=CARTESIAN_POINT('Ctrl Pts',(17.6485150766254,21.6573815714476,0.551458507827716));
#210584=CARTESIAN_POINT('Ctrl Pts',(20.203243920748,21.4476431071891,0.67863431450915));
#210585=CARTESIAN_POINT('Ctrl Pts',(21.4100527174681,19.1863847097626,0.805810121190585));
#210586=CARTESIAN_POINT('Ctrl Pts',(20.1617388348746,16.9474699013169,0.932985927872018));
#210587=CARTESIAN_POINT('Ctrl Pts',(17.6035685870678,16.7853277296908,1.06016173455346));
#210588=CARTESIAN_POINT('Ctrl Pts',(16.0824961952363,18.8485248156151,1.18733754123489));
#210589=CARTESIAN_POINT('Ctrl Pts',(16.994015428193,21.2443038613797,1.31451334791632));
#210590=CARTESIAN_POINT('Ctrl Pts',(19.5018617550643,21.7746354401676,1.44168915459776));
#210591=CARTESIAN_POINT('Ctrl Pts',(21.3052429724622,19.9529996381475,1.56886496127919));
#210592=CARTESIAN_POINT('Ctrl Pts',(20.7496681485409,17.4506205409442,1.69604076796063));
#210593=CARTESIAN_POINT('Ctrl Pts',(18.3448430103915,16.5632827654992,1.82321657464206));
#210594=CARTESIAN_POINT('Ctrl Pts',(16.2970452015994,18.1050599558195,1.9503923813235));
#210595=CARTESIAN_POINT('Ctrl Pts',(16.4850021943108,20.6614691488127,2.07756818800493));
#210596=CARTESIAN_POINT('Ctrl Pts',(18.736275070432,21.8871625843198,2.20474399468636));
#210597=CARTESIAN_POINT('Ctrl Pts',(20.9854607183013,20.6576431264228,2.3319198013678));
#210598=CARTESIAN_POINT('Ctrl Pts',(21.169070894564,18.1009182973116,2.45909560804923));
#210599=CARTESIAN_POINT('Ctrl Pts',(19.1186546646734,16.5626245784783,2.58627141473067));
#210600=CARTESIAN_POINT('Ctrl Pts',(16.7153416532344,17.4540509075189,2.7134472214121));
#210601=CARTESIAN_POINT('Ctrl Pts',(16.1640223834416,19.9573689931488,2.84062302809354));
#210602=CARTESIAN_POINT('Ctrl Pts',(17.9704980657522,21.7759398458068,2.96779883477497));
#210603=CARTESIAN_POINT('Ctrl Pts',(20.4774393846103,21.2413375915055,3.0949746414564));
#210604=CARTESIAN_POINT('Ctrl Pts',(21.384883278063,18.8440266121716,3.22215044813784));
#210605=CARTESIAN_POINT('Ctrl Pts',(19.8603062963049,16.7833909401617,3.34932625481927));
#210606=CARTESIAN_POINT('Ctrl Pts',(17.3024131941191,16.9499359056603,3.4765020615007));
#210607=CARTESIAN_POINT('Ctrl Pts',(16.0579121320417,19.1908668405009,3.60367786818214));
#210608=CARTESIAN_POINT('Ctrl Pts',(17.268555592065,21.4502686994473,3.73085367486357));
#210609=CARTESIAN_POINT('Ctrl Pts',(19.8236533406339,21.6552805114082,3.85802948154501));
#210610=CARTESIAN_POINT('Ctrl Pts',(21.3790617806833,19.6178166632753,3.98520528822644));
#210611=CARTESIAN_POINT('Ctrl Pts',(20.5077902080058,17.2071237764952,4.11238109490788));
#210612=CARTESIAN_POINT('Ctrl Pts',(18.0091762133191,16.634862950186,4.23955690158931));
#210613=CARTESIAN_POINT('Ctrl Pts',(16.1755430552745,18.4260479739882,4.36673270827075));
#210614=CARTESIAN_POINT('Ctrl Pts',(16.6891353482686,20.9373777620364,4.49390851495218));
#210615=CARTESIAN_POINT('Ctrl Pts',(19.0787640406122,21.8648631045058,4.62108432163361));
#210616=CARTESIAN_POINT('Ctrl Pts',(21.1520931241638,20.3575937659115,4.74826012831505));
#210617=CARTESIAN_POINT('Ctrl Pts',(21.0069718500806,17.7983958127287,4.87543593499648));
#210618=CARTESIAN_POINT('Ctrl Pts',(18.7765399800919,16.5351745252634,5.00261174167792));
#210619=CARTESIAN_POINT('Ctrl Pts',(16.5070803186978,17.7268570304097,5.12978754835935));
#210620=CARTESIAN_POINT('Ctrl Pts',(16.280681246675,20.2801485938535,5.25696335504078));
#210621=CARTESIAN_POINT('Ctrl Pts',(18.305049860693,21.8525626812824,5.38413916172222));
#210622=CARTESIAN_POINT('Ctrl Pts',(20.722953603877,21.0015069625052,5.51131496840365));
#210623=CARTESIAN_POINT('Ctrl Pts',(21.3161158638869,18.5077722370249,5.63849077508509));
#210624=CARTESIAN_POINT('Ctrl Pts',(19.5403470829654,16.6592053368368,5.76566658176652));
#210625=CARTESIAN_POINT('Ctrl Pts',(17.0248049009675,17.1517516578618,5.89284238844796));
#210626=CARTESIAN_POINT('Ctrl Pts',(16.0773431377199,19.5335305214322,6.02001819512939));
#210627=CARTESIAN_POINT('Ctrl Pts',(17.5671991548932,21.6194076500902,6.14719400181082));
#210628=CARTESIAN_POINT('Ctrl Pts',(20.127522527624,21.4957202424278,6.27436980849226));
#210629=CARTESIAN_POINT('Ctrl Pts',(21.4093754730223,19.2759438180688,6.40154561517369));
#210630=CARTESIAN_POINT('Ctrl Pts',(20.2367374744517,16.9965854714996,6.52872142185513));
#210631=CARTESIAN_POINT('Ctrl Pts',(17.6854311134782,16.7488150127633,6.65589722853656));
#210632=CARTESIAN_POINT('Ctrl Pts',(16.0961216243634,18.7599464593815,6.78307303521799));
#210633=CARTESIAN_POINT('Ctrl Pts',(16.9269018196985,21.1848915339771,6.91024884189944));
#210634=CARTESIAN_POINT('Ctrl Pts',(19.4155824342976,21.7989136396742,7.03742464858086));
#210635=CARTESIAN_POINT('Ctrl Pts',(21.2789534692056,20.0386856050059,7.1646004552623));
#210636=CARTESIAN_POINT('Ctrl Pts',(20.8074876537439,17.5191073997068,7.29177626194374));
#210637=CARTESIAN_POINT('Ctrl Pts',(18.4337256111302,16.551735644479,7.41895206862516));
#210638=CARTESIAN_POINT('Ctrl Pts',(16.335446683174,18.0240738828814,7.54612787530661));
#210639=CARTESIAN_POINT('Ctrl Pts',(16.4376915523973,20.5853431647969,7.67330368198803));
#210640=CARTESIAN_POINT('Ctrl Pts',(18.64665689732,21.8857378943683,7.80047948866947));
#210641=CARTESIAN_POINT('Ctrl Pts',(20.9357541178272,20.7322266188132,7.92765529535091));
#210642=CARTESIAN_POINT('Ctrl Pts',(21.2048785915005,18.1830843384694,8.05483110203234));
#210643=CARTESIAN_POINT('Ctrl Pts',(19.2071253174932,16.5769908779387,8.18200690871378));
#210644=CARTESIAN_POINT('Ctrl Pts',(16.7753089301549,17.3874373018554,8.3091827153952));
#210645=CARTESIAN_POINT('Ctrl Pts',(16.1404700293211,19.8708893182541,8.43635852207665));
#210646=CARTESIAN_POINT('Ctrl Pts',(17.8850339039608,21.7489338425049,8.56353432875807));
#210647=CARTESIAN_POINT('Ctrl Pts',(20.4084714789379,21.2985815881968,8.69071013543951));
#210648=CARTESIAN_POINT('Ctrl Pts',(21.3956854014105,18.9330027966444,8.81788594212095));
#210649=CARTESIAN_POINT('Ctrl Pts',(19.9409681709163,16.8224691847183,8.94506174880238));
#210650=CARTESIAN_POINT('Ctrl Pts',(17.3789325564997,16.9032643468714,9.07223755548381));
#210651=CARTESIAN_POINT('Ctrl Pts',(16.0600872165237,19.1012637365415,9.19941336216525));
#210652=CARTESIAN_POINT('Ctrl Pts',(17.1943908936429,21.3999393369342,9.32658916884668));
#210653=CARTESIAN_POINT('Ctrl Pts',(19.7411903669265,21.6903989565872,9.45376497552812));
#210654=CARTESIAN_POINT('Ctrl Pts',(21.3639551918393,19.7061639224262,9.58094078220955));
#210655=CARTESIAN_POINT('Ctrl Pts',(20.5738993616681,17.2676467227782,9.70811658889098));
#210656=CARTESIAN_POINT('Ctrl Pts',(18.0958500641997,16.6120355368737,9.83529239557241));
#210657=CARTESIAN_POINT('Ctrl Pts',(16.2032637247762,18.3408129359606,9.96246820225386));
#210658=CARTESIAN_POINT('Ctrl Pts',(16.6324708426624,20.8679329564033,10.0896440089353));
#210659=CARTESIAN_POINT('Ctrl Pts',(18.989700526796,21.8749198302035,10.2168198156167));
#210660=CARTESIAN_POINT('Ctrl Pts',(21.1123408481587,20.4379256013037,10.3439956222982));
#210661=CARTESIAN_POINT('Ctrl Pts',(21.0530010578169,17.8753032847989,10.4711714289796));
#210662=CARTESIAN_POINT('Ctrl Pts',(18.8661217303663,16.5380998018032,10.5983472356611));
#210663=CARTESIAN_POINT('Ctrl Pts',(16.5580289157041,17.6531163517569,10.7255230423425));
#210664=CARTESIAN_POINT('Ctrl Pts',(16.2462545148863,20.1973944558094,10.8526988490239));
#210665=CARTESIAN_POINT('Ctrl Pts',(18.2168321897617,21.8367168692014,10.9798746557054));
#210666=CARTESIAN_POINT('Ctrl Pts',(20.6618792314763,21.0671070254696,11.1070504623868));
#210667=CARTESIAN_POINT('Ctrl Pts',(21.3382167359914,18.5946341888639,11.2342262690682));
#210668=CARTESIAN_POINT('Ctrl Pts',(19.6253470211541,16.6876387279989,11.3614020757497));
#210669=CARTESIAN_POINT('Ctrl Pts',(17.0947217376433,17.0956706167312,11.4885778824311));
#210670=CARTESIAN_POINT('Ctrl Pts',(16.0680325147611,19.4443859224641,11.6157536891125));
#210671=CARTESIAN_POINT('Ctrl Pts',(17.487202990982,21.5789841299002,11.742929495794));
#210672=CARTESIAN_POINT('Ctrl Pts',(20.0502323380272,21.5411038718235,11.8701053024754));
#210673=CARTESIAN_POINT('Ctrl Pts',(21.4057002095246,19.3654979339054,11.9972811091568));
#210674=CARTESIAN_POINT('Ctrl Pts',(20.3100489631998,17.0481497308524,12.1244569158383));
#210675=CARTESIAN_POINT('Ctrl Pts',(17.7684706137698,16.715082408115,12.2516327225197));
#210676=CARTESIAN_POINT('Ctrl Pts',(16.1127055486938,18.6718645618152,12.3788085292011));
#210677=CARTESIAN_POINT('Ctrl Pts',(16.8618154468087,21.1232700175309,12.5059843358826));
#210678=CARTESIAN_POINT('Ctrl Pts',(19.3285384715983,21.8202864210249,12.633160142564));
#210679=CARTESIAN_POINT('Ctrl Pts',(21.2498093499156,20.1234444838084,12.7603359492454));
#210680=CARTESIAN_POINT('Ctrl Pts',(20.8629812984238,17.5894913653894,12.8875117559269));
#210681=CARTESIAN_POINT('Ctrl Pts',(18.5229450451101,16.5431717770494,13.0146875626083));
#210682=CARTESIAN_POINT('Ctrl Pts',(16.37653861336,17.9444189991726,13.1418633692897));
#210683=CARTESIAN_POINT('Ctrl Pts',(16.3929566832965,20.5076756766722,13.2690391759712));
#210684=CARTESIAN_POINT('Ctrl Pts',(18.5571366947732,21.881312901594,13.3962149826526));
#210685=CARTESIAN_POINT('Ctrl Pts',(20.8835778114207,20.8051037776138,13.523390789334));
#210686=CARTESIAN_POINT('Ctrl Pts',(21.2379147039354,18.2664033789119,13.6505665960155));
#210687=CARTESIAN_POINT('Ctrl Pts',(19.2950652660628,16.5943117517799,13.7777424026969));
#210688=CARTESIAN_POINT('Ctrl Pts',(16.8374732702154,17.3228691824008,13.9049182093783));
#210689=CARTESIAN_POINT('Ctrl Pts',(16.119826837221,19.7836694475537,14.0320940160598));
#210690=CARTESIAN_POINT('Ctrl Pts',(17.800522027191,21.7190810384507,14.1592698227412));
#210691=CARTESIAN_POINT('Ctrl Pts',(20.337625319036,21.3534839456345,14.2864456294226));
#210692=CARTESIAN_POINT('Ctrl Pts',(21.4035019128779,19.0222908102495,14.4136214361041));
#210693=CARTESIAN_POINT('Ctrl Pts',(20.0202761896291,16.8642266438473,14.5407972427855));
#210694=CARTESIAN_POINT('Ctrl Pts',(17.4569718976996,16.8591813745337,14.667973049467));
#210695=CARTESIAN_POINT('Ctrl Pts',(16.0652616283277,19.011783723759,14.7951488561484));
#210696=CARTESIAN_POINT('Ctrl Pts',(17.1219531743809,21.347154641679,14.9223246628298));
#210697=CARTESIAN_POINT('Ctrl Pts',(19.6575976280295,21.7227362605683,15.0495004695112));
#210698=CARTESIAN_POINT('Ctrl Pts',(21.3458985828949,19.7939557563202,15.1766762761927));
#210699=CARTESIAN_POINT('Ctrl Pts',(20.6379447006631,17.3303495279633,15.3038520828741));
#210700=CARTESIAN_POINT('Ctrl Pts',(18.1832397277084,16.5921233813674,15.4310278895556));
#210701=CARTESIAN_POINT('Ctrl Pts',(16.2338231205434,18.2565539865522,15.558203696237));
#210702=CARTESIAN_POINT('Ctrl Pts',(16.5781636218018,20.7966295694748,15.6853795029184));
#210703=CARTESIAN_POINT('Ctrl Pts',(18.9003501937609,21.8819884376745,15.8125553095998));
#210704=CARTESIAN_POINT('Ctrl Pts',(21.0699207878016,20.5168811945468,15.9397311162813));
#210705=CARTESIAN_POINT('Ctrl Pts',(21.0964290426296,17.9537090075503,16.0669069229627));
#210706=CARTESIAN_POINT('Ctrl Pts',(18.9555552797279,16.5440232698465,16.1940827296442));
#210707=CARTESIAN_POINT('Ctrl Pts',(16.6114182989473,17.5811231508143,16.3212585363256));
#210708=CARTESIAN_POINT('Ctrl Pts',(16.2146182866043,20.1135338793437,16.448434343007));
#210709=CARTESIAN_POINT('Ctrl Pts',(18.1291946258374,21.8179257911455,16.5756101496885));
#210710=CARTESIAN_POINT('Ctrl Pts',(20.5986423574096,21.1306250936339,16.7027859563699));
#210711=CARTESIAN_POINT('Ctrl Pts',(21.3573964588153,18.6821875180837,16.8299617630513));
#210712=CARTESIAN_POINT('Ctrl Pts',(19.7093471356056,16.7189025728874,16.9571375697328));
#210713=CARTESIAN_POINT('Ctrl Pts',(17.1664773523482,17.0419623400562,17.0843133764142));
#210714=CARTESIAN_POINT('Ctrl Pts',(16.0617123068835,19.3549795345634,17.2114891830956));
#210715=CARTESIAN_POINT('Ctrl Pts',(17.4086053589731,21.5359044424863,17.3386649897771));
#210716=CARTESIAN_POINT('Ctrl Pts',(19.9714657309362,21.5838738242719,17.4658407964585));
#210717=CARTESIAN_POINT('Ctrl Pts',(21.3990281005501,19.4548787494468,17.5930166031399));
#210718=CARTESIAN_POINT('Ctrl Pts',(20.3815925982089,17.1021400588277,17.7201924098214));
#210719=CARTESIAN_POINT('Ctrl Pts',(17.8525931481391,16.6841494736224,17.8473682165028));
#210720=CARTESIAN_POINT('Ctrl Pts',(16.1322297783753,18.5843874123414,17.9745440231842));
#210721=CARTESIAN_POINT('Ctrl Pts',(16.7988291028752,21.0595035082659,18.1017198298657));
#210722=CARTESIAN_POINT('Ctrl Pts',(19.240827615245,21.8387323664387,18.2288956365471));
#210723=CARTESIAN_POINT('Ctrl Pts',(21.2178432478782,20.2071798738389,18.3560714432285));
#210724=CARTESIAN_POINT('Ctrl Pts',(20.9160868653179,17.661694176945,18.48324724991));
#210725=CARTESIAN_POINT('Ctrl Pts',(18.6124012193438,16.53760041183,18.6104230565914));
#210726=CARTESIAN_POINT('Ctrl Pts',(16.4202749074846,17.8661848391805,18.7375988632728));
#210727=CARTESIAN_POINT('Ctrl Pts',(16.3508477617745,20.4285537075334,18.8647746699543));
#210728=CARTESIAN_POINT('Ctrl Pts',(18.4678148800254,21.8738926199146,18.9919504766357));
#210729=CARTESIAN_POINT('Ctrl Pts',(20.8289903235801,20.8761928297688,19.1191262833172));
#210730=CARTESIAN_POINT('Ctrl Pts',(21.2681421768659,18.3507819747449,19.2463020899985));
#210731=CARTESIAN_POINT('Ctrl Pts',(19.3823758659115,16.6145677611307,19.37347789668));
#210732=CARTESIAN_POINT('Ctrl Pts',(16.901764947602,17.260418984728,19.5006537033614));
#210733=CARTESIAN_POINT('Ctrl Pts',(16.1021159552911,19.6958072023018,19.6278295100429));
#210734=CARTESIAN_POINT('Ctrl Pts',(17.71705724637,21.6864149424128,19.7550053167243));
#210735=CARTESIAN_POINT('Ctrl Pts',(20.2649803461583,21.4059830371408,19.8821811234057));
#210736=CARTESIAN_POINT('Ctrl Pts',(21.4083240964178,19.11179058023,20.0093569300872));
#210737=CARTESIAN_POINT('Ctrl Pts',(20.0981412930058,16.9086163213995,20.1365327367686));
#210738=CARTESIAN_POINT('Ctrl Pts',(17.5364438729955,16.8177367384453,20.2637085434501));
#210739=CARTESIAN_POINT('Ctrl Pts',(16.0734291934315,18.9225265902324,20.3908843501315));
#210740=CARTESIAN_POINT('Ctrl Pts',(17.051324400287,21.2919749428039,20.5180601568129));
#210741=CARTESIAN_POINT('Ctrl Pts',(19.5729675169019,21.7522539917445,20.6452359634943));
#210742=CARTESIAN_POINT('Ctrl Pts',(21.3249148532192,19.8810978482246,20.7724117701758));
#210743=CARTESIAN_POINT('Ctrl Pts',(20.6998492888418,17.3951538447513,20.8995875768572));
#210744=CARTESIAN_POINT('Ctrl Pts',(18.2712569980454,16.5751642584499,21.0267633835387));
#210745=CARTESIAN_POINT('Ctrl Pts',(16.2671680460494,18.173335892872,21.1539391902201));
#210746=CARTESIAN_POINT('Ctrl Pts',(16.5263110505858,20.7236048928311,21.2811149969015));
#210747=CARTESIAN_POINT('Ctrl Pts',(18.8107430413917,21.8859505777098,21.408290803583));
#210748=CARTESIAN_POINT('Ctrl Pts',(21.0250158327644,20.594584752017,21.5354666102644));
#210749=CARTESIAN_POINT('Ctrl Pts',(21.1369463112861,18.033114815932,21.6626424169459));
#210750=CARTESIAN_POINT('Ctrl Pts',(19.045243604148,16.5537313076661,21.7898182236272));
#210751=CARTESIAN_POINT('Ctrl Pts',(16.6662107556949,17.5094049812102,21.9169940303087));
#210752=CARTESIAN_POINT('Ctrl Pts',(16.1877691919268,20.0318924082093,22.0441698369901));
#210753=CARTESIAN_POINT('Ctrl Pts',(17.4210581868123,21.2025214152156,22.1289537081111));
#210754=CARTESIAN_POINT('Ctrl Pts',(18.1489775608771,21.3973019939627,22.1713456436716));
#210755=CARTESIAN_POINT('Ctrl Pts',(20.579931224634,20.7654465822185,-0.171094883624917));
#210756=CARTESIAN_POINT('Ctrl Pts',(21.0977302873553,20.150594907745,-0.128684292012742));
#210757=CARTESIAN_POINT('Ctrl Pts',(21.4611752161576,18.3736796382696,-0.0438817648400879));
#210758=CARTESIAN_POINT('Ctrl Pts',(19.5021064059726,16.4608275871995,0.0833126978930438));
#210759=CARTESIAN_POINT('Ctrl Pts',(16.8390405955535,17.0785075195682,0.210488504574479));
#210760=CARTESIAN_POINT('Ctrl Pts',(15.9143177751785,19.6490612161152,0.337664311255912));
#210761=CARTESIAN_POINT('Ctrl Pts',(17.5765589736414,21.8195506449214,0.464840117937347));
#210762=CARTESIAN_POINT('Ctrl Pts',(20.300639162813,21.5959087516894,0.592015924618781));
#210763=CARTESIAN_POINT('Ctrl Pts',(21.5874465446713,19.1847529778785,0.719191731300216));
#210764=CARTESIAN_POINT('Ctrl Pts',(20.2563827312793,16.7974219353056,0.84636753798165));
#210765=CARTESIAN_POINT('Ctrl Pts',(17.5286330099687,16.6245314625761,0.973543344663085));
#210766=CARTESIAN_POINT('Ctrl Pts',(15.9067296997928,18.8244965669171,1.10071915134451));
#210767=CARTESIAN_POINT('Ctrl Pts',(16.8786729611136,21.3790902770145,1.22789495802595));
#210768=CARTESIAN_POINT('Ctrl Pts',(19.5527628208785,21.9445771977858,1.35507076470738));
#210769=CARTESIAN_POINT('Ctrl Pts',(21.4756890285423,20.0021863207324,1.48224657138882));
#210770=CARTESIAN_POINT('Ctrl Pts',(20.8832855040238,17.3339261098018,1.60942237807025));
#210771=CARTESIAN_POINT('Ctrl Pts',(18.3190460418495,16.3877672793826,1.73659818475169));
#210772=CARTESIAN_POINT('Ctrl Pts',(16.1355010228962,18.0317478959283,1.86377399143312));
#210773=CARTESIAN_POINT('Ctrl Pts',(16.3359175647298,20.7576198232253,1.99094979811455));
#210774=CARTESIAN_POINT('Ctrl Pts',(18.7364258833992,22.0645636945266,2.11812560479599));
#210775=CARTESIAN_POINT('Ctrl Pts',(21.1347086127881,20.7535401762524,2.24530141147742));
#210776=CARTESIAN_POINT('Ctrl Pts',(21.3304901904839,18.0273316895207,2.37247721815886));
#210777=CARTESIAN_POINT('Ctrl Pts',(19.1441531769682,16.387065461564,2.49965302484029));
#210778=CARTESIAN_POINT('Ctrl Pts',(16.5815260794188,17.337583873188,2.62682883152173));
#210779=CARTESIAN_POINT('Ctrl Pts',(15.9936602069971,20.0068453174889,2.75400463820316));
#210780=CARTESIAN_POINT('Ctrl Pts',(17.9198860096782,21.9459680716425,2.88118044488459));
#210781=CARTESIAN_POINT('Ctrl Pts',(20.5930108690263,21.3759273750031,3.00835625156603));
#210782=CARTESIAN_POINT('Ctrl Pts',(21.5606086391872,18.8197001804373,3.13553205824747));
#210783=CARTESIAN_POINT('Ctrl Pts',(19.9349684220548,16.6224662845049,3.2627078649289));
#210784=CARTESIAN_POINT('Ctrl Pts',(17.2075142181716,16.8000514095034,3.38988367161033));
#210785=CARTESIAN_POINT('Ctrl Pts',(15.8805159747347,19.1895322262035,3.51705947829177));
#210786=CARTESIAN_POINT('Ctrl Pts',(17.1714122172801,21.5987083927831,3.6442352849732));
#210787=CARTESIAN_POINT('Ctrl Pts',(19.8958857653384,21.8173103069526,3.77141109165464));
#210788=CARTESIAN_POINT('Ctrl Pts',(21.5544012384607,19.6447842803171,3.89858689833607));
#210789=CARTESIAN_POINT('Ctrl Pts',(20.6253736291394,17.0742881001989,4.02576270501751));
#210790=CARTESIAN_POINT('Ctrl Pts',(17.961128106969,16.464092468841,4.15293851169893));
#210791=CARTESIAN_POINT('Ctrl Pts',(16.0059445768151,18.3740140050173,4.28011431838038));
#210792=CARTESIAN_POINT('Ctrl Pts',(16.5535825752176,21.0518182423779,4.4072901250618));
#210793=CARTESIAN_POINT('Ctrl Pts',(19.10161822889,22.0407859964237,4.53446593174324));
#210794=CARTESIAN_POINT('Ctrl Pts',(21.3123869745163,20.4336007350771,4.66164173842467));
#210795=CARTESIAN_POINT('Ctrl Pts',(21.1576457037679,17.7047551824572,4.78881754510611));
#210796=CARTESIAN_POINT('Ctrl Pts',(18.7793599282299,16.3577957618358,4.91599335178754));
#210797=CARTESIAN_POINT('Ctrl Pts',(16.3594592338956,17.6284741399031,5.04316915846899));
#210798=CARTESIAN_POINT('Ctrl Pts',(16.1180523118408,20.3510217719769,5.17034496515041));
#210799=CARTESIAN_POINT('Ctrl Pts',(18.2766150296472,22.0276701859931,5.29752077183185));
#210800=CARTESIAN_POINT('Ctrl Pts',(20.8548000692393,21.1201985266286,5.42469657851329));
#210801=CARTESIAN_POINT('Ctrl Pts',(21.4872826770021,18.4611557173071,5.55187238519472));
#210802=CARTESIAN_POINT('Ctrl Pts',(19.5937993166108,16.4900484967713,5.67904819187615));
#210803=CARTESIAN_POINT('Ctrl Pts',(16.9115034483931,17.0152453991512,5.80622399855758));
#210804=CARTESIAN_POINT('Ctrl Pts',(15.9012350493816,19.5549108639094,5.93339980523902));
#210805=CARTESIAN_POINT('Ctrl Pts',(17.4898526713405,21.7790594565463,6.06057561192046));
#210806=CARTESIAN_POINT('Ctrl Pts',(20.2198982468525,21.6471728895478,6.18775141860188));
#210807=CARTESIAN_POINT('Ctrl Pts',(21.5867244061235,19.2802489023316,6.31492722528333));
#210808=CARTESIAN_POINT('Ctrl Pts',(20.3363529828215,16.8497933452978,6.44210303196475));
#210809=CARTESIAN_POINT('Ctrl Pts',(17.615922151023,16.5855983409401,6.56927883864619));
#210810=CARTESIAN_POINT('Ctrl Pts',(15.9212583499232,18.7300464079656,6.69645464532762));
#210811=CARTESIAN_POINT('Ctrl Pts',(16.8071104343333,21.315739544336,6.82363045200906));
#210812=CARTESIAN_POINT('Ctrl Pts',(19.4607640989881,21.9704647836472,6.95080625869048));
#210813=CARTESIAN_POINT('Ctrl Pts',(21.4476568108885,20.0935523556623,7.07798206537194));
#210814=CARTESIAN_POINT('Ctrl Pts',(20.9449378273356,17.4069529187342,7.20515787205335));
#210815=CARTESIAN_POINT('Ctrl Pts',(18.4138206134801,16.3754547070776,7.3323336787348));
#210816=CARTESIAN_POINT('Ctrl Pts',(16.1764481141826,17.9453933078879,7.45950948541623));
#210817=CARTESIAN_POINT('Ctrl Pts',(16.2854707305501,20.6764474963007,7.58668529209767));
#210818=CARTESIAN_POINT('Ctrl Pts',(18.640866978772,22.0630445627872,7.7138610987791));
#210819=CARTESIAN_POINT('Ctrl Pts',(21.0817069934834,20.8330677607659,7.84103690546054));
#210820=CARTESIAN_POINT('Ctrl Pts',(21.3686715568034,18.1149444651214,7.96821271214196));
#210821=CARTESIAN_POINT('Ctrl Pts',(19.2384884929154,16.4023840938492,8.0953885188234));
#210822=CARTESIAN_POINT('Ctrl Pts',(16.6454685488647,17.2665544941074,8.22256432550484));
#210823=CARTESIAN_POINT('Ctrl Pts',(15.9685465823494,19.9146329601232,8.34974013218628));
#210824=CARTESIAN_POINT('Ctrl Pts',(17.8287564831316,21.9171718576127,8.47691593886771));
#210825=CARTESIAN_POINT('Ctrl Pts',(20.5194711248913,21.4369660397109,8.60409174554914));
#210826=CARTESIAN_POINT('Ctrl Pts',(21.5721268283993,18.9145745394082,8.73126755223057));
#210827=CARTESIAN_POINT('Ctrl Pts',(20.0209773208683,16.6641350009595,8.858443358912));
#210828=CARTESIAN_POINT('Ctrl Pts',(17.2891060002617,16.7502860228609,8.98561916559344));
#210829=CARTESIAN_POINT('Ctrl Pts',(15.8828352441794,19.0939893896534,9.11279497227487));
#210830=CARTESIAN_POINT('Ctrl Pts',(17.0923311883199,21.5450427289413,9.23997077895631));
#210831=CARTESIAN_POINT('Ctrl Pts',(19.8079563737189,21.8547567314554,9.36714658563774));
#210832=CARTESIAN_POINT('Ctrl Pts',(21.5382932434809,19.7389880229077,9.49432239231918));
#210833=CARTESIAN_POINT('Ctrl Pts',(20.6958651164175,17.1388230739748,9.62149819900061));
#210834=CARTESIAN_POINT('Ctrl Pts',(18.0535475121228,16.439751840865,9.74867400568204));
#210835=CARTESIAN_POINT('Ctrl Pts',(16.035502831811,18.2831287907025,9.87584981236349));
#210836=CARTESIAN_POINT('Ctrl Pts',(16.4931618156892,20.9777699848882,10.0030256190449));
#210837=CARTESIAN_POINT('Ctrl Pts',(19.0066507515693,22.0515093760514,10.1302014257263));
#210838=CARTESIAN_POINT('Ctrl Pts',(21.2699995454986,20.5192577165824,10.2573772324077));
#210839=CARTESIAN_POINT('Ctrl Pts',(21.2067261583164,17.7867608017806,10.3845530390892));
#210840=CARTESIAN_POINT('Ctrl Pts',(18.874879995573,16.3609149530909,10.5117288457706));
#210841=CARTESIAN_POINT('Ctrl Pts',(16.4137851808899,17.5498452387121,10.6389046524521));
#210842=CARTESIAN_POINT('Ctrl Pts',(16.0813434539675,20.2627819149227,10.7660804591335));
#210843=CARTESIAN_POINT('Ctrl Pts',(18.1825494655964,22.0107739651396,10.8932562658149));
#210844=CARTESIAN_POINT('Ctrl Pts',(20.7896771156604,21.1901471759111,11.0204320724963));
#210845=CARTESIAN_POINT('Ctrl Pts',(21.5108486018171,18.5537756925119,11.1476078791778));
#210846=CARTESIAN_POINT('Ctrl Pts',(19.6844338464684,16.5203667192919,11.2747836858592));
#210847=CARTESIAN_POINT('Ctrl Pts',(16.9860550275624,16.9554467815862,11.4019594925407));
#210848=CARTESIAN_POINT('Ctrl Pts',(15.8913072311674,19.4598569263539,11.5291352992221));
#210849=CARTESIAN_POINT('Ctrl Pts',(17.4045536127647,21.7359562869947,11.6563111059035));
#210850=CARTESIAN_POINT('Ctrl Pts',(20.1374845399016,21.6955649707794,11.783486912585));
#210851=CARTESIAN_POINT('Ctrl Pts',(21.5828055117534,19.3757395033677,11.9106627192664));
#210852=CARTESIAN_POINT('Ctrl Pts',(20.4145242433828,16.9047757665027,12.0378385259478));
#210853=CARTESIAN_POINT('Ctrl Pts',(17.7044662868062,16.5496296234525,12.1650143326293));
#210854=CARTESIAN_POINT('Ctrl Pts',(15.9389416120162,18.6361256176097,12.2921901393107));
#210855=CARTESIAN_POINT('Ctrl Pts',(16.7377095273126,21.2500331768819,12.4193659459921));
#210856=CARTESIAN_POINT('Ctrl Pts',(19.3679500475393,21.9932543530368,12.5465417526735));
#210857=CARTESIAN_POINT('Ctrl Pts',(21.416580746526,20.183929846461,12.673717559355));
#210858=CARTESIAN_POINT('Ctrl Pts',(21.004110110314,17.4820025925939,12.8008933660364));
#210859=CARTESIAN_POINT('Ctrl Pts',(18.5089543468127,16.3663231463401,12.9280691727179));
#210860=CARTESIAN_POINT('Ctrl Pts',(16.2202640022022,17.8604581527614,13.0552449793993));
#210861=CARTESIAN_POINT('Ctrl Pts',(16.2377704155193,20.5936314799435,13.1824207860807));
#210862=CARTESIAN_POINT('Ctrl Pts',(18.5454125391162,22.0583262400653,13.3095965927622));
#210863=CARTESIAN_POINT('Ctrl Pts',(21.0260719530159,20.9107758999245,13.4367723994436));
#210864=CARTESIAN_POINT('Ctrl Pts',(21.4038976120531,18.2037866715935,13.563948206125));
#210865=CARTESIAN_POINT('Ctrl Pts',(19.3322579245662,16.4208531573659,13.6911240128065));
#210866=CARTESIAN_POINT('Ctrl Pts',(16.7117537233642,17.1977061952114,13.8182998194879));
#210867=CARTESIAN_POINT('Ctrl Pts',(15.9465349662162,19.8216313398441,13.9454756261693));
#210868=CARTESIAN_POINT('Ctrl Pts',(17.7386423679729,21.8853401302251,14.0726514328508));
#210869=CARTESIAN_POINT('Ctrl Pts',(20.4439286182524,21.495507839393,14.1998272395322));
#210870=CARTESIAN_POINT('Ctrl Pts',(21.5804614914246,19.0097813984656,14.3270030462136));
#210871=CARTESIAN_POINT('Ctrl Pts',(20.1055426175397,16.708660535411,14.4541788528951));
#210872=CARTESIAN_POINT('Ctrl Pts',(17.3723185195974,16.7032808184137,14.5813546595765));
#210873=CARTESIAN_POINT('Ctrl Pts',(15.8883526644403,18.9985778039157,14.708530466258));
#210874=CARTESIAN_POINT('Ctrl Pts',(17.0150916188663,21.4887589699166,14.8357062729394));
#210875=CARTESIAN_POINT('Ctrl Pts',(19.7188223254962,21.8892376546847,14.9628820796208));
#210876=CARTESIAN_POINT('Ctrl Pts',(21.5190396734505,19.8325995214557,15.0900578863023));
#210877=CARTESIAN_POINT('Ctrl Pts',(20.7641559800708,17.2056824081085,15.2172336929837));
#210878=CARTESIAN_POINT('Ctrl Pts',(18.1467301806671,16.4185197212751,15.3444094996651));
#210879=CARTESIAN_POINT('Ctrl Pts',(16.0680879904256,18.1932843692987,15.4715853063465));
#210880=CARTESIAN_POINT('Ctrl Pts',(16.4352546038082,20.9017399419349,15.598761113028));
#210881=CARTESIAN_POINT('Ctrl Pts',(18.9113774419666,22.0590465570016,15.7259369197094));
#210882=CARTESIAN_POINT('Ctrl Pts',(21.2247674864064,20.6034472257245,15.8531127263909));
#210883=CARTESIAN_POINT('Ctrl Pts',(21.2530329565334,17.870363989867,15.9802885330723));
#210884=CARTESIAN_POINT('Ctrl Pts',(18.9702420378592,16.3672310840514,16.1074643397537));
#210885=CARTESIAN_POINT('Ctrl Pts',(16.4707137122836,17.4730796544138,16.2346401464351));
#210886=CARTESIAN_POINT('Ctrl Pts',(16.0476100802981,20.1733622743496,16.3618159531166));
#210887=CARTESIAN_POINT('Ctrl Pts',(18.0891024634763,21.9907372385088,16.488991759798));
#210888=CARTESIAN_POINT('Ctrl Pts',(20.7222483095596,21.2578758162869,16.6161675664795));
#210889=CARTESIAN_POINT('Ctrl Pts',(21.5312997362295,18.6471328760627,16.7433433731609));
#210890=CARTESIAN_POINT('Ctrl Pts',(19.7740022749111,16.5537030245103,16.8705191798423));
#210891=CARTESIAN_POINT('Ctrl Pts',(17.0625672761828,16.8981782175187,16.9976949865238));
#210892=CARTESIAN_POINT('Ctrl Pts',(15.8845680607422,19.3645238460445,17.1248707932052));
#210893=CARTESIAN_POINT('Ctrl Pts',(17.3207457938787,21.6900208745888,17.2520465998866));
#210894=CARTESIAN_POINT('Ctrl Pts',(20.053496544683,21.7411701160866,17.3792224065681));
#210895=CARTESIAN_POINT('Ctrl Pts',(21.5756911129322,19.4710453161425,17.5063982132495));
#210896=CARTESIAN_POINT('Ctrl Pts',(20.4908104603086,16.9623450788714,17.6335740199309));
#210897=CARTESIAN_POINT('Ctrl Pts',(17.794165250305,16.516646164469,17.7607498266124));
#210898=CARTESIAN_POINT('Ctrl Pts',(15.959760090426,18.5428496637114,17.8879256332938));
#210899=CARTESIAN_POINT('Ctrl Pts',(16.6705478588277,21.1820396264035,18.0151014399752));
#210900=CARTESIAN_POINT('Ctrl Pts',(19.2744248944815,22.0129230684028,18.1422772466567));
#210901=CARTESIAN_POINT('Ctrl Pts',(21.3824956319804,20.2732160020698,18.2694530533381));
#210902=CARTESIAN_POINT('Ctrl Pts',(21.0607360113538,17.5589916824588,18.3966288600195));
#210903=CARTESIAN_POINT('Ctrl Pts',(18.6043405137593,16.360382458875,18.523804666701));
#210904=CARTESIAN_POINT('Ctrl Pts',(16.2668995473587,17.7770379002201,18.6509804733824));
#210905=CARTESIAN_POINT('Ctrl Pts',(16.1928701204568,20.5092645659538,18.7781562800638));
#210906=CARTESIAN_POINT('Ctrl Pts',(18.45016963826,22.0504140726478,18.9053320867453));
#210907=CARTESIAN_POINT('Ctrl Pts',(20.9678658954356,20.9865773999889,19.0325078934267));
#210908=CARTESIAN_POINT('Ctrl Pts',(21.4361288448778,18.2937586707072,19.1596837001081));
#210909=CARTESIAN_POINT('Ctrl Pts',(19.4253562883709,16.4424519246523,19.2868595067896));
#210910=CARTESIAN_POINT('Ctrl Pts',(16.780307255024,17.1311162137809,19.414035313471));
#210911=CARTESIAN_POINT('Ctrl Pts',(15.9276500412235,19.7279447624144,19.5412111201524));
#210912=CARTESIAN_POINT('Ctrl Pts',(17.6496447600855,21.8505086195232,19.6683869268339));
#210913=CARTESIAN_POINT('Ctrl Pts',(20.3664680564733,21.5514870621786,19.7955627335153));
#210914=CARTESIAN_POINT('Ctrl Pts',(21.5856033344346,19.1052140510933,19.9227385401968));
#210915=CARTESIAN_POINT('Ctrl Pts',(20.1885693489379,16.7559927763657,20.0499143468782));
#210916=CARTESIAN_POINT('Ctrl Pts',(17.457058641429,16.6590888438425,20.1770901535596));
#210917=CARTESIAN_POINT('Ctrl Pts',(15.8970616522235,18.9034038719576,20.3042659602411));
#210918=CARTESIAN_POINT('Ctrl Pts',(16.9397809084021,21.4299214440102,20.4314417669225));
#210919=CARTESIAN_POINT('Ctrl Pts',(19.6285821382997,21.9207120974271,20.5586175736039));
#210920=CARTESIAN_POINT('Ctrl Pts',(21.4966649457231,19.9255182070319,20.6857933802854));
#210921=CARTESIAN_POINT('Ctrl Pts',(20.8301641839021,17.2747825617085,20.8129691869668));
#210922=CARTESIAN_POINT('Ctrl Pts',(18.240582059696,16.40043638892,20.9401449936482));
#210923=CARTESIAN_POINT('Ctrl Pts',(16.1036433297677,18.104549801285,21.0673208003297));
#210924=CARTESIAN_POINT('Ctrl Pts',(16.3799647587305,20.8238745060694,21.1944966070111));
#210925=CARTESIAN_POINT('Ctrl Pts',(18.8158302886401,22.0632713447716,21.3216724136925));
#210926=CARTESIAN_POINT('Ctrl Pts',(21.176885810551,20.6863017024412,21.4488482203739));
#210927=CARTESIAN_POINT('Ctrl Pts',(21.2962360890773,17.9550335586219,21.5760240270554));
#210928=CARTESIAN_POINT('Ctrl Pts',(19.06587574408,16.377582661504,21.7031998337368));
#210929=CARTESIAN_POINT('Ctrl Pts',(16.529138326029,17.396607333106,21.8303756404183));
#210930=CARTESIAN_POINT('Ctrl Pts',(16.0189811762652,20.0863088421845,21.9575514470997));
#210931=CARTESIAN_POINT('Ctrl Pts',(17.3340241117299,21.3345380991533,22.0423353182207));
#210932=CARTESIAN_POINT('Ctrl Pts',(18.1101967966574,21.5422305581871,22.0847272537811));
#210933=CARTESIAN_POINT('Ctrl Pts',(20.6946895702226,20.8620838326754,-0.257713273515286));
#210934=CARTESIAN_POINT('Ctrl Pts',(21.2446793034262,20.2090078950206,-0.21530268190311));
#210935=CARTESIAN_POINT('Ctrl Pts',(21.6307189736713,18.3216248822974,-0.130500154730457));
#210936=CARTESIAN_POINT('Ctrl Pts',(19.54985825025,16.2898541338203,-0.00330569199732536));
#210937=CARTESIAN_POINT('Ctrl Pts',(16.7212342529824,16.9459341572626,0.123870114684109));
#210938=CARTESIAN_POINT('Ctrl Pts',(15.7390230172331,19.6762947228445,0.251045921365543));
#210939=CARTESIAN_POINT('Ctrl Pts',(17.5046028706573,21.9817197183951,0.378221728046977));
#210940=CARTESIAN_POINT('Ctrl Pts',(20.3980344048781,21.7441743961897,0.505397534728411));
#210941=CARTESIAN_POINT('Ctrl Pts',(21.7648403718746,19.1831212459942,0.632573341409846));
#210942=CARTESIAN_POINT('Ctrl Pts',(20.3510266276838,16.6473739692942,0.75974914809128));
#210943=CARTESIAN_POINT('Ctrl Pts',(17.4536974328697,16.4637351954612,0.886924954772715));
#210944=CARTESIAN_POINT('Ctrl Pts',(15.7309632043494,18.8004683182191,1.01410076145415));
#210945=CARTESIAN_POINT('Ctrl Pts',(16.7633304940341,21.5138766926494,1.14127656813558));
#210946=CARTESIAN_POINT('Ctrl Pts',(19.6036638866926,22.1145189554039,1.26845237481702));
#210947=CARTESIAN_POINT('Ctrl Pts',(21.6461350846223,20.0513730033173,1.39562818149845));
#210948=CARTESIAN_POINT('Ctrl Pts',(21.016902859507,17.2172316786593,1.52280398817988));
#210949=CARTESIAN_POINT('Ctrl Pts',(18.2932490733073,16.2122517932659,1.64997979486132));
#210950=CARTESIAN_POINT('Ctrl Pts',(15.9739568441929,17.9584358360373,1.77715560154276));
#210951=CARTESIAN_POINT('Ctrl Pts',(16.1868329351487,20.853770497638,1.90433140822419));
#210952=CARTESIAN_POINT('Ctrl Pts',(18.7365766963666,22.2419648047335,2.03150721490562));
#210953=CARTESIAN_POINT('Ctrl Pts',(21.2839565072747,20.8494372260819,2.15868302158706));
#210954=CARTESIAN_POINT('Ctrl Pts',(21.4919094864037,17.9537450817297,2.28585882826849));
#210955=CARTESIAN_POINT('Ctrl Pts',(19.169651689263,16.2115063446496,2.41303463494992));
#210956=CARTESIAN_POINT('Ctrl Pts',(16.4477105056032,17.2211168388571,2.54021044163136));
#210957=CARTESIAN_POINT('Ctrl Pts',(15.8232980305525,20.0563216418289,2.66738624831279));
#210958=CARTESIAN_POINT('Ctrl Pts',(17.8692739536042,22.1159962974782,2.79456205499423));
#210959=CARTESIAN_POINT('Ctrl Pts',(20.7085823534422,21.5105171585006,2.92173786167567));
#210960=CARTESIAN_POINT('Ctrl Pts',(21.7363340003116,18.7953737487032,3.04891366835709));
#210961=CARTESIAN_POINT('Ctrl Pts',(20.0096305478046,16.4615416288479,3.17608947503854));
#210962=CARTESIAN_POINT('Ctrl Pts',(17.1126152422242,16.6501669133465,3.30326528171996));
#210963=CARTESIAN_POINT('Ctrl Pts',(15.7031198174278,19.1881976119062,3.4304410884014));
#210964=CARTESIAN_POINT('Ctrl Pts',(17.0742688424951,21.7471480861189,3.55761689508284));
#210965=CARTESIAN_POINT('Ctrl Pts',(19.9681181900429,21.9793401024969,3.68479270176427));
#210966=CARTESIAN_POINT('Ctrl Pts',(21.7297406962381,19.671751897359,3.8119685084457));
#210967=CARTESIAN_POINT('Ctrl Pts',(20.742957050273,16.9414524239027,3.93914431512714));
#210968=CARTESIAN_POINT('Ctrl Pts',(17.9130800006189,16.2933219874959,4.06632012180857));
#210969=CARTESIAN_POINT('Ctrl Pts',(15.8363460983557,18.3219800360464,4.19349592849001));
#210970=CARTESIAN_POINT('Ctrl Pts',(16.4180298021666,21.1662587227194,4.32067173517144));
#210971=CARTESIAN_POINT('Ctrl Pts',(19.1244724171678,22.2167088883417,4.44784754185288));
#210972=CARTESIAN_POINT('Ctrl Pts',(21.4726808248689,20.5096077042429,4.57502334853431));
#210973=CARTESIAN_POINT('Ctrl Pts',(21.3083195574551,17.6111145521858,4.70219915521574));
#210974=CARTESIAN_POINT('Ctrl Pts',(18.7821798763678,16.1804169984081,4.82937496189718));
#210975=CARTESIAN_POINT('Ctrl Pts',(16.2118381490933,17.5300912493964,4.95655076857861));
#210976=CARTESIAN_POINT('Ctrl Pts',(15.9554233770066,20.4218949501003,5.08372657526004));
#210977=CARTESIAN_POINT('Ctrl Pts',(18.2481801986013,22.2027776907038,5.21090238194148));
#210978=CARTESIAN_POINT('Ctrl Pts',(20.9866465346018,21.238890090752,5.33807818862291));
#210979=CARTESIAN_POINT('Ctrl Pts',(21.6584494901173,18.4145391975892,5.46525399530435));
#210980=CARTESIAN_POINT('Ctrl Pts',(19.6472515502562,16.3208916567058,5.59242980198579));
#210981=CARTESIAN_POINT('Ctrl Pts',(16.7982019958189,16.8787391404406,5.71960560866721));
#210982=CARTESIAN_POINT('Ctrl Pts',(15.7251269610433,19.5762912063867,5.84678141534867));
#210983=CARTESIAN_POINT('Ctrl Pts',(17.4125061877879,21.9387112630022,5.97395722203007));
#210984=CARTESIAN_POINT('Ctrl Pts',(20.3122739660809,21.7986255366678,6.10113302871153));
#210985=CARTESIAN_POINT('Ctrl Pts',(21.7640733392246,19.2845539865944,6.22830883539295));
#210986=CARTESIAN_POINT('Ctrl Pts',(20.4359684911912,16.703001219096,6.35548464207439));
#210987=CARTESIAN_POINT('Ctrl Pts',(17.5464131885678,16.422381669117,6.48266044875582));
#210988=CARTESIAN_POINT('Ctrl Pts',(15.7463950754831,18.7001463565497,6.60983625543726));
#210989=CARTESIAN_POINT('Ctrl Pts',(16.6873190489681,21.4465875546951,6.7370120621187));
#210990=CARTESIAN_POINT('Ctrl Pts',(19.5059457636785,22.1420159276201,6.86418786880012));
#210991=CARTESIAN_POINT('Ctrl Pts',(21.6163601525715,20.1484191063189,6.99136367548156));
#210992=CARTESIAN_POINT('Ctrl Pts',(21.0823880009273,17.2947984377616,7.118539482163));
#210993=CARTESIAN_POINT('Ctrl Pts',(18.3939156158299,16.1991737696759,7.24571528884443));
#210994=CARTESIAN_POINT('Ctrl Pts',(16.0174495451912,17.8667127328943,7.37289109552587));
#210995=CARTESIAN_POINT('Ctrl Pts',(16.1332499087027,20.7675518278046,7.50006690220729));
#210996=CARTESIAN_POINT('Ctrl Pts',(18.6350770602241,22.2403512312061,7.62724270888874));
#210997=CARTESIAN_POINT('Ctrl Pts',(21.2276598691396,20.9339089027185,7.75441851557016));
#210998=CARTESIAN_POINT('Ctrl Pts',(21.5324645221063,18.0468045917732,7.8815943222516));
#210999=CARTESIAN_POINT('Ctrl Pts',(19.2698516683375,16.2277773097598,8.00877012893304));
#211000=CARTESIAN_POINT('Ctrl Pts',(16.5156281675744,17.1456716863595,8.13594593561446));
#211001=CARTESIAN_POINT('Ctrl Pts',(15.7966231353776,19.9583766019922,8.26312174229592));
#211002=CARTESIAN_POINT('Ctrl Pts',(17.7724790623024,22.0854098727205,8.39029754897732));
#211003=CARTESIAN_POINT('Ctrl Pts',(20.6304707708447,21.5753504912249,8.51747335565878));
#211004=CARTESIAN_POINT('Ctrl Pts',(21.7485682553881,18.8961462821721,8.64464916234021));
#211005=CARTESIAN_POINT('Ctrl Pts',(20.1009864708203,16.5058008172007,8.77182496902164));
#211006=CARTESIAN_POINT('Ctrl Pts',(17.199279444024,16.5973076988504,8.89900077570308));
#211007=CARTESIAN_POINT('Ctrl Pts',(15.705583271835,19.0867150427652,9.0261765823845));
#211008=CARTESIAN_POINT('Ctrl Pts',(16.9902714829968,21.6901461209486,9.15335238906595));
#211009=CARTESIAN_POINT('Ctrl Pts',(19.8747223805114,22.0191145063235,9.28052819574737));
#211010=CARTESIAN_POINT('Ctrl Pts',(21.7126312951226,19.7718121233893,9.40770400242882));
#211011=CARTESIAN_POINT('Ctrl Pts',(20.8178308711669,17.0099994251714,9.53487980911025));
#211012=CARTESIAN_POINT('Ctrl Pts',(18.011244960046,16.2674681448564,9.66205561579168));
#211013=CARTESIAN_POINT('Ctrl Pts',(15.8677419388458,18.2254446454444,9.78923142247312));
#211014=CARTESIAN_POINT('Ctrl Pts',(16.353852788716,21.0876070133732,9.91640722915455));
#211015=CARTESIAN_POINT('Ctrl Pts',(19.0236009763425,22.2280989218993,10.043583035836));
#211016=CARTESIAN_POINT('Ctrl Pts',(21.4276582428386,20.6005898318611,10.1707588425174));
#211017=CARTESIAN_POINT('Ctrl Pts',(21.3604512588158,17.6982183187623,10.2979346491988));
#211018=CARTESIAN_POINT('Ctrl Pts',(18.8836382607796,16.1837301043787,10.4251104558803));
#211019=CARTESIAN_POINT('Ctrl Pts',(16.2695414460758,17.4465741256675,10.5522862625617));
#211020=CARTESIAN_POINT('Ctrl Pts',(15.9164323930488,20.3281693740358,10.6794620692432));
#211021=CARTESIAN_POINT('Ctrl Pts',(18.1482667414313,22.1848310610778,10.8066378759246));
#211022=CARTESIAN_POINT('Ctrl Pts',(20.9174749998444,21.3131873263528,10.933813682606));
#211023=CARTESIAN_POINT('Ctrl Pts',(21.6834804676428,18.5129171961597,11.0609894892874));
#211024=CARTESIAN_POINT('Ctrl Pts',(19.7435206717827,16.3530947105848,11.1881652959689));
#211025=CARTESIAN_POINT('Ctrl Pts',(16.8773883174812,16.8152229464412,11.3153411026503));
#211026=CARTESIAN_POINT('Ctrl Pts',(15.7145819475737,19.4753279302436,11.4425169093318));
#211027=CARTESIAN_POINT('Ctrl Pts',(17.3219042345475,21.8929284440893,11.5696927160132));
#211028=CARTESIAN_POINT('Ctrl Pts',(20.2247367417761,21.8500260697353,11.6968685226946));
#211029=CARTESIAN_POINT('Ctrl Pts',(21.7599108139823,19.3859810728298,11.824044329376));
#211030=CARTESIAN_POINT('Ctrl Pts',(20.5189995235657,16.7614018021532,11.9512201360575));
#211031=CARTESIAN_POINT('Ctrl Pts',(17.6404619598426,16.38417683879,12.0783959427389));
#211032=CARTESIAN_POINT('Ctrl Pts',(15.7651776753385,18.6003866734043,12.2055717494204));
#211033=CARTESIAN_POINT('Ctrl Pts',(16.6136036078165,21.3767963362328,12.3327475561018));
#211034=CARTESIAN_POINT('Ctrl Pts',(19.4073616234801,22.1662222850487,12.4599233627832));
#211035=CARTESIAN_POINT('Ctrl Pts',(21.5833521431366,20.2444152091134,12.5870991694647));
#211036=CARTESIAN_POINT('Ctrl Pts',(21.1452389222041,17.3745138197983,12.7142749761461));
#211037=CARTESIAN_POINT('Ctrl Pts',(18.4949636485153,16.1894745156307,12.8414507828275));
#211038=CARTESIAN_POINT('Ctrl Pts',(16.0639893910444,17.7764973063501,12.968626589509));
#211039=CARTESIAN_POINT('Ctrl Pts',(16.0825841477421,20.6795872832148,13.0958023961904));
#211040=CARTESIAN_POINT('Ctrl Pts',(18.5336883834592,22.2353395785366,13.2229782028718));
#211041=CARTESIAN_POINT('Ctrl Pts',(21.1685660946113,21.0164480222352,13.3501540095533));
#211042=CARTESIAN_POINT('Ctrl Pts',(21.5698805201709,18.1411699642751,13.4773298162347));
#211043=CARTESIAN_POINT('Ctrl Pts',(19.3694505830695,16.247394562952,13.6045056229161));
#211044=CARTESIAN_POINT('Ctrl Pts',(16.5860341765131,17.072543208022,13.7316814295976));
#211045=CARTESIAN_POINT('Ctrl Pts',(15.7732430952114,19.8595932321345,13.858857236279));
#211046=CARTESIAN_POINT('Ctrl Pts',(17.6767627087548,22.0515992219996,13.9860330429604));
#211047=CARTESIAN_POINT('Ctrl Pts',(20.5502319174689,21.6375317331515,14.1132088496419));
#211048=CARTESIAN_POINT('Ctrl Pts',(21.7574210699713,18.9972719866817,14.2403846563233));
#211049=CARTESIAN_POINT('Ctrl Pts',(20.1908090454502,16.5530944269748,14.3675604630048));
#211050=CARTESIAN_POINT('Ctrl Pts',(17.2876651414952,16.5473802622938,14.4947362696862));
#211051=CARTESIAN_POINT('Ctrl Pts',(15.7114437005529,18.9853718840723,14.6219120763676));
#211052=CARTESIAN_POINT('Ctrl Pts',(16.9082300633519,21.6303632981543,14.749087883049));
#211053=CARTESIAN_POINT('Ctrl Pts',(19.7800470229629,22.0557390488012,14.8762636897305));
#211054=CARTESIAN_POINT('Ctrl Pts',(21.692180764006,19.8712432865912,15.0034394964119));
#211055=CARTESIAN_POINT('Ctrl Pts',(20.8903672594785,17.0810152882537,15.1306153030934));
#211056=CARTESIAN_POINT('Ctrl Pts',(18.1102206336258,16.2449160611827,15.2577911097748));
#211057=CARTESIAN_POINT('Ctrl Pts',(15.9023528603076,18.1300147520451,15.3849669164562));
#211058=CARTESIAN_POINT('Ctrl Pts',(16.2923455858144,21.0068503143949,15.5121427231376));
#211059=CARTESIAN_POINT('Ctrl Pts',(18.9224046901724,22.2361046763285,15.6393185298191));
#211060=CARTESIAN_POINT('Ctrl Pts',(21.379614185011,20.6900132569022,15.7664943365005));
#211061=CARTESIAN_POINT('Ctrl Pts',(21.4096368704371,17.7870189721836,15.8936701431819));
#211062=CARTESIAN_POINT('Ctrl Pts',(18.9849287959905,16.1904388982563,16.0208459498634));
#211063=CARTESIAN_POINT('Ctrl Pts',(16.33000912562,17.3650361580133,16.1480217565448));
#211064=CARTESIAN_POINT('Ctrl Pts',(15.8806018739919,20.2331906693557,16.2751975632263));
#211065=CARTESIAN_POINT('Ctrl Pts',(18.0490103011151,22.1635486858722,16.4023733699077));
#211066=CARTESIAN_POINT('Ctrl Pts',(20.8458542617096,21.3851265389399,16.5295491765891));
#211067=CARTESIAN_POINT('Ctrl Pts',(21.7052030136437,18.6120782340418,16.6567249832706));
#211068=CARTESIAN_POINT('Ctrl Pts',(19.8386574142166,16.3885034761332,16.783900789952));
#211069=CARTESIAN_POINT('Ctrl Pts',(16.9586572000173,16.754394094981,16.9110765966334));
#211070=CARTESIAN_POINT('Ctrl Pts',(15.7074238146008,19.3740681575255,17.0382524033149));
#211071=CARTESIAN_POINT('Ctrl Pts',(17.2328862287842,21.8441373066915,17.1654282099963));
#211072=CARTESIAN_POINT('Ctrl Pts',(20.1355273584301,21.8984664079011,17.2926040166777));
#211073=CARTESIAN_POINT('Ctrl Pts',(21.7523541253142,19.487211882838,17.4197798233592));
#211074=CARTESIAN_POINT('Ctrl Pts',(20.6000283224083,16.8225500989152,17.5469556300406));
#211075=CARTESIAN_POINT('Ctrl Pts',(17.7357373524709,16.3491428553155,17.674131436722));
#211076=CARTESIAN_POINT('Ctrl Pts',(15.7872904024767,18.5013119150815,17.8013072434035));
#211077=CARTESIAN_POINT('Ctrl Pts',(16.5422666147802,21.304575744541,17.9284830500849));
#211078=CARTESIAN_POINT('Ctrl Pts',(19.3080221737182,22.1871137703668,18.0556588567663));
#211079=CARTESIAN_POINT('Ctrl Pts',(21.5471480160826,20.3392521303006,18.1828346634478));
#211080=CARTESIAN_POINT('Ctrl Pts',(21.2053851573897,17.4562891879729,18.3100104701292));
#211081=CARTESIAN_POINT('Ctrl Pts',(18.5962798081749,16.1831645059201,18.4371862768106));
#211082=CARTESIAN_POINT('Ctrl Pts',(16.1135241872327,17.6878909612598,18.5643620834921));
#211083=CARTESIAN_POINT('Ctrl Pts',(16.0348924791393,20.5899754243741,18.6915378901735));
#211084=CARTESIAN_POINT('Ctrl Pts',(18.4325243964945,22.226935525381,18.8187136968549));
#211085=CARTESIAN_POINT('Ctrl Pts',(21.1067414672911,21.0969619702091,18.9458895035364));
#211086=CARTESIAN_POINT('Ctrl Pts',(21.6041155128897,18.2367353666694,19.0730653102178));
#211087=CARTESIAN_POINT('Ctrl Pts',(19.4683367108302,16.270336088174,19.2002411168992));
#211088=CARTESIAN_POINT('Ctrl Pts',(16.6588495624458,17.0018134428338,19.3274169235807));
#211089=CARTESIAN_POINT('Ctrl Pts',(15.7531841271558,19.760082322527,19.4545927302621));
#211090=CARTESIAN_POINT('Ctrl Pts',(17.5822322738009,22.0146022966338,19.5817685369435));
#211091=CARTESIAN_POINT('Ctrl Pts',(20.4679557667883,21.6969910872163,19.708944343625));
#211092=CARTESIAN_POINT('Ctrl Pts',(21.7628825724515,19.0986375219567,19.8361201503064));
#211093=CARTESIAN_POINT('Ctrl Pts',(20.2789974048699,16.6033692313319,19.9632959569879));
#211094=CARTESIAN_POINT('Ctrl Pts',(17.3776734098626,16.5004409492398,20.0904717636693));
#211095=CARTESIAN_POINT('Ctrl Pts',(15.7206941110155,18.8842811536826,20.2176475703507));
#211096=CARTESIAN_POINT('Ctrl Pts',(16.8282374165171,21.5678679452165,20.3448233770321));
#211097=CARTESIAN_POINT('Ctrl Pts',(19.6841967596975,22.0891702031096,20.4719991837136));
#211098=CARTESIAN_POINT('Ctrl Pts',(21.668415038227,19.9699385658392,20.5991749903951));
#211099=CARTESIAN_POINT('Ctrl Pts',(20.9604790789623,17.1544112786656,20.7263507970764));
#211100=CARTESIAN_POINT('Ctrl Pts',(18.2099071213465,16.2257085193901,20.8535266037579));
#211101=CARTESIAN_POINT('Ctrl Pts',(15.9401186134861,18.0357637096982,20.9807024104393));
#211102=CARTESIAN_POINT('Ctrl Pts',(16.233618466875,20.9241441193076,21.1078782171208));
#211103=CARTESIAN_POINT('Ctrl Pts',(18.8209175358886,22.2405921118336,21.2350540238022));
#211104=CARTESIAN_POINT('Ctrl Pts',(21.3287557883375,20.7780186528654,21.3622298304836));
#211105=CARTESIAN_POINT('Ctrl Pts',(21.4555258668686,17.8769523013118,21.4894056371651));
#211106=CARTESIAN_POINT('Ctrl Pts',(19.0865078840121,16.2014340153418,21.6165814438465));
#211107=CARTESIAN_POINT('Ctrl Pts',(16.3920658963632,17.2838096850018,21.7437572505279));
#211108=CARTESIAN_POINT('Ctrl Pts',(15.8501931606037,20.1407252761597,21.8709330572094));
#211109=CARTESIAN_POINT('Ctrl Pts',(17.2469900366476,21.4665547830909,21.9557169283303));
#211110=CARTESIAN_POINT('Ctrl Pts',(18.0714160324376,21.6871591224115,21.9981088638908));
#211111=CARTESIAN_POINT('Ctrl Pts',(20.3539256943887,20.5739122292573,2.60208521396521E-18));
#211112=CARTESIAN_POINT('Ctrl Pts',(20.4076089227952,20.5221116197655,-8.76976867613359E-16));
#211113=CARTESIAN_POINT('Ctrl Pts',(20.4581355934374,20.4674384227593,-2.52590746105995E-14));
#211114=CARTESIAN_POINT('Ctrl Pts',(20.505511973405,20.410263943529,-1.70176372993325E-15));
#211115=CARTESIAN_POINT('Ctrl Pts',(20.5545756561021,20.3510532037207,2.26945372756332E-14));
#211116=CARTESIAN_POINT('Ctrl Pts',(20.6002611628448,20.2891594084515,2.60865837895201E-14));
#211117=CARTESIAN_POINT('Ctrl Pts',(20.642547115175,20.2249453565119,1.84262327618256E-14));
#211118=CARTESIAN_POINT('Ctrl Pts',(20.6826816163244,20.163998427346,1.11556298740125E-14));
#211119=CARTESIAN_POINT('Ctrl Pts',(20.719753745937,20.1009604021271,-8.83402169628207E-15));
#211120=CARTESIAN_POINT('Ctrl Pts',(20.753716758437,20.0361087206568,9.29811783123569E-15));
#211121=CARTESIAN_POINT('Ctrl Pts',(20.7688150794711,20.0072787837823,1.71471824035106E-14));
#211122=CARTESIAN_POINT('Ctrl Pts',(20.7832985639006,19.9780900549027,2.84583620301588E-14));
#211123=CARTESIAN_POINT('Ctrl Pts',(20.7971611119739,19.9485653699547,5.09314812546791E-15));
#211124=CARTESIAN_POINT('Ctrl Pts',(20.8039895160331,19.9340221216659,-6.39236290215152E-15));
#211125=CARTESIAN_POINT('Ctrl Pts',(20.8106672398928,19.9193973462958,1.44353959261987E-14));
#211126=CARTESIAN_POINT('Ctrl Pts',(20.8171934366481,19.9046937060787,1.06720188242093E-14));
#211127=CARTESIAN_POINT('Ctrl Pts',(20.8232055554644,19.8911482928261,7.48952413932212E-15));
#211128=CARTESIAN_POINT('Ctrl Pts',(20.8290895460591,19.8775345581707,1.69617332493456E-15));
#211129=CARTESIAN_POINT('Ctrl Pts',(20.8348368052234,19.8638741231809,4.37844205336546E-15));
#211130=CARTESIAN_POINT('Ctrl Pts',(20.8659056669685,19.7900277637342,1.88375660372629E-14));
#211131=CARTESIAN_POINT('Ctrl Pts',(20.8930393190126,19.7146930410775,3.61062706447889E-14));
#211132=CARTESIAN_POINT('Ctrl Pts',(20.9162161295942,19.6382510927703,1.90264470845136E-14));
#211133=CARTESIAN_POINT('Ctrl Pts',(20.9398193031497,19.5604029105767,1.63242134604958E-15));
#211134=CARTESIAN_POINT('Ctrl Pts',(20.959319229244,19.4814055816633,1.27489672905939E-14));
#211135=CARTESIAN_POINT('Ctrl Pts',(20.9746521650443,19.4016261052126,4.85722573273506E-16));
#211136=CARTESIAN_POINT('Ctrl Pts',(20.9885844253233,19.32913454552,-1.06572652727376E-14));
#211137=CARTESIAN_POINT('Ctrl Pts',(20.9990759703875,19.2559962568405,3.89867626280975E-15));
#211138=CARTESIAN_POINT('Ctrl Pts',(21.0060451898833,19.1824707413237,1.37806432931598E-14));
#211139=CARTESIAN_POINT('Ctrl Pts',(21.0087031237876,19.1544294433498,1.74701789075424E-14));
#211140=CARTESIAN_POINT('Ctrl Pts',(21.0108483731097,19.1263317159654,-5.7355876066468E-15));
#211141=CARTESIAN_POINT('Ctrl Pts',(21.0124750503239,19.0981916687962,1.26704202685346E-14));
#211142=CARTESIAN_POINT('Ctrl Pts',(21.0133685656744,19.0827346599387,2.28408658292894E-14));
#211143=CARTESIAN_POINT('Ctrl Pts',(21.0141056048104,19.0672648807305,-1.46450263791898E-15));
#211144=CARTESIAN_POINT('Ctrl Pts',(21.0146850898148,19.0517846622215,5.06539254985228E-15));
#211145=CARTESIAN_POINT('Ctrl Pts',(21.0151328036157,19.0398245469222,1.02796891611799E-14));
#211146=CARTESIAN_POINT('Ctrl Pts',(21.0154863000461,19.0278615000918,2.25762263693188E-14));
#211147=CARTESIAN_POINT('Ctrl Pts',(21.015745158205,19.0159051388708,1.90403248723214E-14));
#211148=CARTESIAN_POINT('Ctrl Pts',(21.017551908051,18.9324534374073,-5.41087435524647E-15));
#211149=CARTESIAN_POINT('Ctrl Pts',(21.014756822678,18.8492079748143,-1.7965889298872E-14));
#211150=CARTESIAN_POINT('Ctrl Pts',(21.0073036571099,18.7665493842094,-9.43689570931383E-16));
#211151=CARTESIAN_POINT('Ctrl Pts',(20.9998648139147,18.6840496344554,1.63477607125224E-14));
#211152=CARTESIAN_POINT('Ctrl Pts',(20.9877861501509,18.60213349936,6.07683838498736E-15));
#211153=CARTESIAN_POINT('Ctrl Pts',(20.9709623839625,18.5211637972932,9.07607322631065E-15));
#211154=CARTESIAN_POINT('Ctrl Pts',(20.9545246627898,18.4420520591064,1.2427326863693E-14));
#211155=CARTESIAN_POINT('Ctrl Pts',(20.9335573250132,18.3638428657348,-1.29184203455733E-14));
#211156=CARTESIAN_POINT('Ctrl Pts',(20.9083260331535,18.2867626991381,-6.38378239159465E-16));
#211157=CARTESIAN_POINT('Ctrl Pts',(20.8979286030734,18.2549991395388,4.51921879028503E-15));
#211158=CARTESIAN_POINT('Ctrl Pts',(20.886806477603,18.223427374722,1.48021303909579E-14));
#211159=CARTESIAN_POINT('Ctrl Pts',(20.8749757625748,18.1920637286001,7.49400541621981E-15));
#211160=CARTESIAN_POINT('Ctrl Pts',(20.868424493201,18.1746960805925,3.22326148169017E-15));
#211161=CARTESIAN_POINT('Ctrl Pts',(20.8616536960862,18.1573871105346,8.68449611504115E-15));
#211162=CARTESIAN_POINT('Ctrl Pts',(20.8546784987878,18.1401696684741,5.24580379135386E-15));
#211163=CARTESIAN_POINT('Ctrl Pts',(20.8237193197693,18.06375062996,-9.59599133981877E-15));
#211164=CARTESIAN_POINT('Ctrl Pts',(20.7887042347096,17.9890383341861,1.00214989038782E-14));
#211165=CARTESIAN_POINT('Ctrl Pts',(20.7499612622237,17.916256394916,1.44606548957427E-14));
#211166=CARTESIAN_POINT('Ctrl Pts',(20.7091543143746,17.8395971039635,1.91363004497942E-14));
#211167=CARTESIAN_POINT('Ctrl Pts',(20.6642116622635,17.7650784733303,-4.62531541653634E-15));
#211168=CARTESIAN_POINT('Ctrl Pts',(20.6154560962815,17.692967425201,1.04916075827077E-14));
#211169=CARTESIAN_POINT('Ctrl Pts',(20.5667005302995,17.6208563770717,2.56085305819518E-14));
#211170=CARTESIAN_POINT('Ctrl Pts',(20.5141314518022,17.55115202568,2.07608830934162E-14));
#211171=CARTESIAN_POINT('Ctrl Pts',(20.4580183994378,17.484139989662,2.21211937656562E-14));
#211172=CARTESIAN_POINT('Ctrl Pts',(20.4361046684505,17.457969897886,2.30143573901407E-14));
#211173=CARTESIAN_POINT('Ctrl Pts',(20.4136499126721,17.4322106904206,1.67053283342637E-15));
#211174=CARTESIAN_POINT('Ctrl Pts',(20.3906682863214,17.4068806089605,9.04831765069503E-15));
#211175=CARTESIAN_POINT('Ctrl Pts',(20.3815365196799,17.3968156819022,1.20932955461059E-14));
#211176=CARTESIAN_POINT('Ctrl Pts',(20.3723208008609,17.3868177123508,-1.58786556649917E-14));
#211177=CARTESIAN_POINT('Ctrl Pts',(20.3630243250802,17.3768903879953,-1.62370117351429E-14));
#211178=CARTESIAN_POINT('Ctrl Pts',(20.3025146980146,17.3122746444938,-1.87508807042265E-14));
#211179=CARTESIAN_POINT('Ctrl Pts',(20.2387852814275,17.2508599884964,-1.29144917290363E-14));
#211180=CARTESIAN_POINT('Ctrl Pts',(20.1721441631346,17.1929207844063,-2.06501482580279E-14));
#211181=CARTESIAN_POINT('Ctrl Pts',(20.116951256814,17.1449348990317,-2.70569039828667E-14));
#211182=CARTESIAN_POINT('Ctrl Pts',(20.0597599943144,17.0993329745171,2.10331963193576E-15));
#211183=CARTESIAN_POINT('Ctrl Pts',(20.0007222400369,17.0562848434724,1.38777878078145E-15));
#211184=CARTESIAN_POINT('Ctrl Pts',(19.9812253415778,17.0420684314475,1.43084424546213E-15));
#211185=CARTESIAN_POINT('Ctrl Pts',(19.9615269094649,17.0281306668005,8.22589116977551E-16));
#211186=CARTESIAN_POINT('Ctrl Pts',(19.9416319850871,17.0144780743264,5.05151476204446E-15));
#211187=CARTESIAN_POINT('Ctrl Pts',(19.9257068710494,17.0035497044602,8.2357117562639E-15));
#211188=CARTESIAN_POINT('Ctrl Pts',(19.9096544915251,16.9928033016912,1.13873654213532E-14));
#211189=CARTESIAN_POINT('Ctrl Pts',(19.8934933769624,16.9822523936718,9.85322934354826E-15));
#211190=CARTESIAN_POINT('Ctrl Pts',(19.8189655612139,16.9335963355889,2.49494022146064E-15));
#211191=CARTESIAN_POINT('Ctrl Pts',(19.7420556121672,16.8890439678595,-1.1204578293946E-14));
#211192=CARTESIAN_POINT('Ctrl Pts',(19.6630443965311,16.8488858958507,-3.58046925441613E-15));
#211193=CARTESIAN_POINT('Ctrl Pts',(19.5852031544112,16.8093224720868,4.67551488835544E-15));
#211194=CARTESIAN_POINT('Ctrl Pts',(19.5053217346575,16.774023445591,-1.3425717557294E-14));
#211195=CARTESIAN_POINT('Ctrl Pts',(19.423636270734,16.7433040636654,1.66533453693773E-16));
#211196=CARTESIAN_POINT('Ctrl Pts',(19.4149415054419,16.7400342307853,1.73416518801677E-15));
#211197=CARTESIAN_POINT('Ctrl Pts',(19.4062262753773,16.736816326208,1.52237426317155E-14));
#211198=CARTESIAN_POINT('Ctrl Pts',(19.3974909960169,16.7336502196964,1.0547118733939E-15));
#211199=CARTESIAN_POINT('Ctrl Pts',(18.071416109725,16.7348411664207,0.0018909634849847));
#211200=CARTESIAN_POINT('Ctrl Pts',(17.2469902101003,16.9554454800088,0.0442828990454628));
#211201=CARTESIAN_POINT('Ctrl Pts',(15.8501940740727,18.2812783317349,0.129066770166419));
#211202=CARTESIAN_POINT('Ctrl Pts',(16.3920656588252,21.1381881653492,0.256242576847853));
#211203=CARTESIAN_POINT('Ctrl Pts',(19.0865079389648,22.2205670934987,0.383418383529288));
#211204=CARTESIAN_POINT('Ctrl Pts',(21.4555257828913,20.5450469055032,0.510594190210721));
#211205=CARTESIAN_POINT('Ctrl Pts',(21.3287556324384,17.643981848867,0.637769996892157));
#211206=CARTESIAN_POINT('Ctrl Pts',(18.8209175760198,16.1814077573175,0.76494580357359));
#211207=CARTESIAN_POINT('Ctrl Pts',(16.233618537572,17.4978560985894,0.892121610255025));
#211208=CARTESIAN_POINT('Ctrl Pts',(15.9401187499945,20.386236157729,1.01929741693646));
#211209=CARTESIAN_POINT('Ctrl Pts',(18.2099071291442,22.1962914055474,1.1464732236179));
#211210=CARTESIAN_POINT('Ctrl Pts',(20.9604789958506,21.2675886098998,1.27364903029933));
#211211=CARTESIAN_POINT('Ctrl Pts',(21.6684149124547,18.4520614803885,1.40082483698077));
#211212=CARTESIAN_POINT('Ctrl Pts',(19.6841967236086,16.3328299069189,1.5280006436622));
#211213=CARTESIAN_POINT('Ctrl Pts',(16.8282374931634,16.8541321563464,1.65517645034364));
#211214=CARTESIAN_POINT('Ctrl Pts',(15.7206942359514,19.5377188303282,1.78235225702507));
#211215=CARTESIAN_POINT('Ctrl Pts',(17.3776734650805,21.9215589406766,1.90952806370651));
#211216=CARTESIAN_POINT('Ctrl Pts',(20.2789973416443,21.8186306606476,2.03670387038793));
#211217=CARTESIAN_POINT('Ctrl Pts',(21.7628824476932,19.3233624738419,2.16387967706937));
#211218=CARTESIAN_POINT('Ctrl Pts',(20.4679556955709,16.7250090148042,2.2910554837508));
#211219=CARTESIAN_POINT('Ctrl Pts',(17.5822323211178,16.4073978188031,2.41823129043224));
#211220=CARTESIAN_POINT('Ctrl Pts',(15.7531842497881,18.6619176999891,2.54540709711367));
#211221=CARTESIAN_POINT('Ctrl Pts',(16.65884964778,21.4201864663384,2.67258290379511));
#211222=CARTESIAN_POINT('Ctrl Pts',(19.468336680636,22.1516637908563,2.79975871047654));
#211223=CARTESIAN_POINT('Ctrl Pts',(21.6041153948362,20.1852645932698,2.92693451715798));
#211224=CARTESIAN_POINT('Ctrl Pts',(21.1067413697027,17.3250381073553,3.05411032383941));
#211225=CARTESIAN_POINT('Ctrl Pts',(18.432524408893,16.1950645986679,3.18128613052084));
#211226=CARTESIAN_POINT('Ctrl Pts',(16.0348925901549,17.8320246323415,3.30846193720228));
#211227=CARTESIAN_POINT('Ctrl Pts',(16.1135242950128,20.7341089760952,3.43563774388371));
#211228=CARTESIAN_POINT('Ctrl Pts',(18.5962798138393,22.2388353695441,3.56281355056515));
#211229=CARTESIAN_POINT('Ctrl Pts',(21.2053850557409,20.9657107398561,3.68998935724659));
#211230=CARTESIAN_POINT('Ctrl Pts',(21.5471479003775,18.0827479161047,3.81716516392802));
#211231=CARTESIAN_POINT('Ctrl Pts',(19.3080221501088,16.2348863520412,3.94434097060946));
#211232=CARTESIAN_POINT('Ctrl Pts',(16.5422667049268,17.1174243415679,4.07151677729088));
#211233=CARTESIAN_POINT('Ctrl Pts',(15.7872905236753,19.9206880557286,4.19869258397231));
#211234=CARTESIAN_POINT('Ctrl Pts',(17.7357373935294,22.0728570269757,4.32586839065375));
#211235=CARTESIAN_POINT('Ctrl Pts',(20.6000282456582,21.5994498028477,4.45304419733518));
#211236=CARTESIAN_POINT('Ctrl Pts',(21.7523540011689,18.9347881285228,4.58022000401662));
#211237=CARTESIAN_POINT('Ctrl Pts',(20.1355273007852,16.5235337026348,4.70739581069805));
#211238=CARTESIAN_POINT('Ctrl Pts',(17.2328862905255,16.5778628016098,4.83457161737948));
#211239=CARTESIAN_POINT('Ctrl Pts',(15.7074239390844,19.0479318491813,4.96174742406093));
#211240=CARTESIAN_POINT('Ctrl Pts',(16.9586572730372,21.6676058039782,5.08892323074235));
#211241=CARTESIAN_POINT('Ctrl Pts',(19.8386573687817,22.0334964077772,5.21609903742379));
#211242=CARTESIAN_POINT('Ctrl Pts',(21.7052028914376,19.8099217413247,5.34327484410521));
#211243=CARTESIAN_POINT('Ctrl Pts',(20.8458541748489,17.0368735504825,5.47045065078667));
#211244=CARTESIAN_POINT('Ctrl Pts',(18.0490103292891,16.2584514355665,5.59762645746809));
#211245=CARTESIAN_POINT('Ctrl Pts',(15.8806019913527,18.188809372687,5.72480226414953));
#211246=CARTESIAN_POINT('Ctrl Pts',(16.3300092244964,21.0569637660617,5.85197807083096));
#211247=CARTESIAN_POINT('Ctrl Pts',(18.9849287856695,22.2315609775075,5.97915387751239));
#211248=CARTESIAN_POINT('Ctrl Pts',(21.4096367603877,20.634980969248,6.10632968419384));
#211249=CARTESIAN_POINT('Ctrl Pts',(21.3796140761966,17.73198680393,6.23350549087526));
#211250=CARTESIAN_POINT('Ctrl Pts',(18.9224046824235,16.1858954480944,6.3606812975567));
#211251=CARTESIAN_POINT('Ctrl Pts',(16.2923456862402,17.4151497594685,6.48785710423813));
#211252=CARTESIAN_POINT('Ctrl Pts',(15.9023529767735,20.2919852034935,6.61503291091956));
#211253=CARTESIAN_POINT('Ctrl Pts',(18.1102206592817,22.1770838168218,6.74220871760101));
#211254=CARTESIAN_POINT('Ctrl Pts',(20.8903671707866,21.3409846241399,6.86938452428244));
#211255=CARTESIAN_POINT('Ctrl Pts',(21.6921806423356,18.550756740565,6.99656033096387));
#211256=CARTESIAN_POINT('Ctrl Pts',(19.7800469799392,16.3662610682035,7.12373613764531));
#211257=CARTESIAN_POINT('Ctrl Pts',(16.9082301384463,16.7916368013544,7.25091194432673));
#211258=CARTESIAN_POINT('Ctrl Pts',(15.7114438248711,19.4366281066474,7.37808775100818));
#211259=CARTESIAN_POINT('Ctrl Pts',(17.2876652009831,21.8746196281511,7.50526355768959));
#211260=CARTESIAN_POINT('Ctrl Pts',(20.1908089855312,21.8689054637052,7.63243936437105));
#211261=CARTESIAN_POINT('Ctrl Pts',(21.7574209456176,19.4247280045279,7.75961517105247));
#211262=CARTESIAN_POINT('Ctrl Pts',(20.5502318427671,16.7844683666522,7.88679097773391));
#211263=CARTESIAN_POINT('Ctrl Pts',(17.6767627522393,16.3704008948346,8.01396678441534));
#211264=CARTESIAN_POINT('Ctrl Pts',(15.7732432169878,18.562406794542,8.14114259109678));
#211265=CARTESIAN_POINT('Ctrl Pts',(16.5860342648591,21.3494567040227,8.26831839777821));
#211266=CARTESIAN_POINT('Ctrl Pts',(19.3694505569332,22.1746053151545,8.39549420445964));
#211267=CARTESIAN_POINT('Ctrl Pts',(21.5698804035306,20.2808299917227,8.52267001114109));
#211268=CARTESIAN_POINT('Ctrl Pts',(21.1685659944773,17.4055520520233,8.64984581782252));
#211269=CARTESIAN_POINT('Ctrl Pts',(18.5336883916982,16.1866605458549,8.77702162450395));
#211270=CARTESIAN_POINT('Ctrl Pts',(16.0825842567954,17.7424127771882,8.90419743118537));
#211271=CARTESIAN_POINT('Ctrl Pts',(16.0639895008622,20.6455026346484,9.03137323786683));
#211272=CARTESIAN_POINT('Ctrl Pts',(18.4949636583467,22.2325253600935,9.15854904454826));
#211273=CARTESIAN_POINT('Ctrl Pts',(21.1452388230294,21.0474861046668,9.28572485122969));
#211274=CARTESIAN_POINT('Ctrl Pts',(21.5833520259422,18.1775848333912,9.41290065791111));
#211275=CARTESIAN_POINT('Ctrl Pts',(19.4073615957849,16.2557778365002,9.54007646459256));
#211276=CARTESIAN_POINT('Ctrl Pts',(16.6136036950289,17.0452037528466,9.66725227127399));
#211277=CARTESIAN_POINT('Ctrl Pts',(15.7651777974467,19.8216133014809,9.79442807795543));
#211278=CARTESIAN_POINT('Ctrl Pts',(17.6404620048199,22.0378230449422,9.92160388463686));
#211279=CARTESIAN_POINT('Ctrl Pts',(20.5189994501482,21.6605980970946,10.0487796913183));
#211280=CARTESIAN_POINT('Ctrl Pts',(21.7599106895262,19.0360189343673,10.1759554979997));
#211281=CARTESIAN_POINT('Ctrl Pts',(20.2247366804621,16.5719740388084,10.3031313046812));
#211282=CARTESIAN_POINT('Ctrl Pts',(17.3219042926274,16.5290716662188,10.4303071113626));
#211283=CARTESIAN_POINT('Ctrl Pts',(15.7145820717629,18.9466720806279,10.557482918044));
#211284=CARTESIAN_POINT('Ctrl Pts',(16.8773883938439,21.60677695502,10.6846587247255));
#211285=CARTESIAN_POINT('Ctrl Pts',(19.7435206302607,22.0689051718692,10.8118345314069));
#211286=CARTESIAN_POINT('Ctrl Pts',(21.6834803463302,19.9090827751282,10.9390103380884));
#211287=CARTESIAN_POINT('Ctrl Pts',(20.9174749100379,17.1088127601106,11.0661861447698));
#211288=CARTESIAN_POINT('Ctrl Pts',(18.1482667655227,16.2371690612364,11.1933619514512));
#211289=CARTESIAN_POINT('Ctrl Pts',(15.9164325089359,18.0938306719134,11.3205377581326));
#211290=CARTESIAN_POINT('Ctrl Pts',(16.2695415474392,20.9754258017613,11.4477135648141));
#211291=CARTESIAN_POINT('Ctrl Pts',(18.8836382546247,22.2382697711092,11.5748893714955));
#211292=CARTESIAN_POINT('Ctrl Pts',(21.3604511507894,20.7237816190169,11.702065178177));
#211293=CARTESIAN_POINT('Ctrl Pts',(21.4276581320481,17.8214102252931,11.8292409848584));
#211294=CARTESIAN_POINT('Ctrl Pts',(19.0236009644314,16.1939012021945,11.9564167915398));
#211295=CARTESIAN_POINT('Ctrl Pts',(16.353852886612,17.3343930638118,12.0835925982213));
#211296=CARTESIAN_POINT('Ctrl Pts',(15.8677420567354,20.1965553140193,12.2107684049027));
#211297=CARTESIAN_POINT('Ctrl Pts',(18.0112449897728,22.1545317340756,12.3379442115841));
#211298=CARTESIAN_POINT('Ctrl Pts',(20.8178307854584,21.4120004843013,12.4651200182656));
#211299=CARTESIAN_POINT('Ctrl Pts',(21.712631172611,18.6501878996771,12.592295824947));
#211300=CARTESIAN_POINT('Ctrl Pts',(19.8747223335935,16.4028856091748,12.7194716316284));
#211301=CARTESIAN_POINT('Ctrl Pts',(16.9902715547168,16.731853981019,12.8466474383099));
#211302=CARTESIAN_POINT('Ctrl Pts',(15.7055833963943,19.3352849521227,12.9738232449913));
#211303=CARTESIAN_POINT('Ctrl Pts',(17.199279507147,21.824692193648,13.1009990516727));
#211304=CARTESIAN_POINT('Ctrl Pts',(20.1009864145957,21.9161990715341,13.2281748583542));
#211305=CARTESIAN_POINT('Ctrl Pts',(21.7485681313984,19.5258537048782,13.3553506650356));
#211306=CARTESIAN_POINT('Ctrl Pts',(20.6304706928427,16.8466496060213,13.482526471717));
#211307=CARTESIAN_POINT('Ctrl Pts',(17.77247910185,16.3365902455044,13.6097022783985));
#211308=CARTESIAN_POINT('Ctrl Pts',(15.7966232561924,18.4636234287474,13.7368780850799));
#211309=CARTESIAN_POINT('Ctrl Pts',(16.5156282588163,21.2763282286931,13.8640538917614));
#211310=CARTESIAN_POINT('Ctrl Pts',(19.2698516462976,22.1942225675398,13.9912296984428));
#211311=CARTESIAN_POINT('Ctrl Pts',(21.5324644070049,20.3751953603434,14.1184055051242));
#211312=CARTESIAN_POINT('Ctrl Pts',(21.2276597665751,17.4880911681452,14.2455813118056));
#211313=CARTESIAN_POINT('Ctrl Pts',(18.635077064293,16.1816488933915,14.3727571184871));
#211314=CARTESIAN_POINT('Ctrl Pts',(16.1332500156721,17.6544482362164,14.4999329251685));
#211315=CARTESIAN_POINT('Ctrl Pts',(16.0174496569233,20.5552872118146,14.6271087318499));
#211316=CARTESIAN_POINT('Ctrl Pts',(18.3939156298175,22.2228261064472,14.7542845385314));
#211317=CARTESIAN_POINT('Ctrl Pts',(21.0823879043376,21.1272014834248,14.8814603452128));
#211318=CARTESIAN_POINT('Ctrl Pts',(21.6163600340197,18.2735809322375,15.0086361518943));
#211319=CARTESIAN_POINT('Ctrl Pts',(19.5059457319285,16.279984192933,15.1358119585757));
#211320=CARTESIAN_POINT('Ctrl Pts',(16.6873191331485,16.975412537255,15.2629877652571));
#211321=CARTESIAN_POINT('Ctrl Pts',(15.7463951983637,19.7218536224386,15.3901635719385));
#211322=CARTESIAN_POINT('Ctrl Pts',(17.5464132374134,21.9996182161866,15.51733937862));
#211323=CARTESIAN_POINT('Ctrl Pts',(20.4359684211888,21.7189986777498,15.6445151853014));
#211324=CARTESIAN_POINT('Ctrl Pts',(21.7640732145973,19.137446016431,15.7716909919829));
#211325=CARTESIAN_POINT('Ctrl Pts',(20.3122739011665,16.6233745697617,15.8988667986643));
#211326=CARTESIAN_POINT('Ctrl Pts',(17.4125062421414,16.4832888491888,16.0260426053457));
#211327=CARTESIAN_POINT('Ctrl Pts',(15.7251270847987,18.8457088086375,16.1532184120272));
#211328=CARTESIAN_POINT('Ctrl Pts',(16.7982020754384,21.543260763633,16.2803942187086));
#211329=CARTESIAN_POINT('Ctrl Pts',(19.6472515126938,22.1011082244237,16.40757002539));
#211330=CARTESIAN_POINT('Ctrl Pts',(21.6584493698341,20.0074607696524,16.5347458320715));
#211331=CARTESIAN_POINT('Ctrl Pts',(20.9866464419502,17.1831099926555,16.6619216387529));
#211332=CARTESIAN_POINT('Ctrl Pts',(18.2481802185833,16.2192224323484,16.7890974454343));
#211333=CARTESIAN_POINT('Ctrl Pts',(15.9554234912899,18.0001050997038,16.9162732521158));
#211334=CARTESIAN_POINT('Ctrl Pts',(16.2118382528302,20.8919086814673,17.0434490587972));
#211335=CARTESIAN_POINT('Ctrl Pts',(18.782179874386,22.2415828769435,17.1706248654786));
#211336=CARTESIAN_POINT('Ctrl Pts',(21.3083194515728,20.8108853820109,17.2978006721601));
#211337=CARTESIAN_POINT('Ctrl Pts',(21.4726807122266,17.9123923491693,17.4249764788415));
#211338=CARTESIAN_POINT('Ctrl Pts',(19.1244724011078,16.2052912352836,17.552152285523));
#211339=CARTESIAN_POINT('Ctrl Pts',(16.418029897423,17.2557413577005,17.6793280922044));
#211340=CARTESIAN_POINT('Ctrl Pts',(15.8363462175366,20.1000199273879,17.8065038988858));
#211341=CARTESIAN_POINT('Ctrl Pts',(17.9130800343833,22.1286778924994,17.9336797055672));
#211342=CARTESIAN_POINT('Ctrl Pts',(20.7429569676441,21.4805474827506,18.0608555122487));
#211343=CARTESIAN_POINT('Ctrl Pts',(21.7297405730228,18.7502481215919,18.1880313189301));
#211344=CARTESIAN_POINT('Ctrl Pts',(19.9681181392836,16.4426600113656,18.3152071256115));
#211345=CARTESIAN_POINT('Ctrl Pts',(17.0742689107603,16.6748520181929,18.442382932293));
#211346=CARTESIAN_POINT('Ctrl Pts',(15.7031199420884,19.2338023871561,18.5695587389744));
#211347=CARTESIAN_POINT('Ctrl Pts',(17.1126153089119,21.7718329813254,18.6967345456558));
#211348=CARTESIAN_POINT('Ctrl Pts',(20.0096304953375,21.9604582580674,18.8239103523373));
#211349=CARTESIAN_POINT('Ctrl Pts',(21.7363338768253,19.6266262342004,18.9510861590187));
#211350=CARTESIAN_POINT('Ctrl Pts',(20.708582272227,16.9114829360825,19.0782619657001));
#211351=CARTESIAN_POINT('Ctrl Pts',(17.8692739891718,16.3060038219983,19.2054377723816));
#211352=CARTESIAN_POINT('Ctrl Pts',(15.8232981502683,18.3656783929507,19.332613579063));
#211353=CARTESIAN_POINT('Ctrl Pts',(16.4477105996423,21.200883079277,19.4597893857445));
#211354=CARTESIAN_POINT('Ctrl Pts',(19.1696516713374,22.2104935320204,19.5869651924259));
#211355=CARTESIAN_POINT('Ctrl Pts',(21.4919093729839,20.4682548664865,19.7141409991073));
#211356=CARTESIAN_POINT('Ctrl Pts',(21.2839564023691,17.5725628414412,19.8413168057888));
#211357=CARTESIAN_POINT('Ctrl Pts',(18.7365766963097,16.1800353196856,19.9684926124702));
#211358=CARTESIAN_POINT('Ctrl Pts',(16.186833039821,17.5682295703764,20.0956684191516));
#211359=CARTESIAN_POINT('Ctrl Pts',(15.9739569578914,20.4635641116309,20.222844225833));
#211360=CARTESIAN_POINT('Ctrl Pts',(18.2932490910976,22.2097480848697,20.3500200325145));
#211361=CARTESIAN_POINT('Ctrl Pts',(21.0169027662538,21.2047682366741,20.4771958391959));
#211362=CARTESIAN_POINT('Ctrl Pts',(21.6461349636216,18.3706270360342,20.6043716458773));
#211363=CARTESIAN_POINT('Ctrl Pts',(19.6036638532537,16.3074811554586,20.7315474525588));
#211364=CARTESIAN_POINT('Ctrl Pts',(16.7633305706532,16.9081234172833,20.8587232592402));
#211365=CARTESIAN_POINT('Ctrl Pts',(15.7309633363042,19.6215316380409,20.9858990659217));
#211366=CARTESIAN_POINT('Ctrl Pts',(17.4536974694716,21.9582647385426,21.1130748726031));
#211367=CARTESIAN_POINT('Ctrl Pts',(20.3510265917206,21.7746258438458,21.2402506792845));
#211368=CARTESIAN_POINT('Ctrl Pts',(21.7648401891172,19.2388788921253,21.367426485966));
#211369=CARTESIAN_POINT('Ctrl Pts',(20.3980344469297,16.677825473566,21.4946022926474));
#211370=CARTESIAN_POINT('Ctrl Pts',(17.5046027110691,16.4402807821758,21.6217780993288));
#211371=CARTESIAN_POINT('Ctrl Pts',(15.7390235403886,18.7457046750729,21.7489539060103));
#211372=CARTESIAN_POINT('Ctrl Pts',(16.7212335728181,21.4760667201902,21.8761297126917));
#211373=CARTESIAN_POINT('Ctrl Pts',(19.5498596762323,22.1321442401452,22.0033055193731));
#211374=CARTESIAN_POINT('Ctrl Pts',(21.6307161859342,20.100377524994,22.1304999838292));
#211375=CARTESIAN_POINT('Ctrl Pts',(21.2446789959721,18.2129921435845,22.2153025127247));
#211376=CARTESIAN_POINT('Ctrl Pts',(20.6946892744878,17.5599162803241,22.2577131060598));
#211377=CARTESIAN_POINT('Ctrl Pts',(18.1101968784744,16.8797697475724,-0.0847274365222671));
#211378=CARTESIAN_POINT('Ctrl Pts',(17.3340242953481,17.0874621793657,-0.0423355009617889));
#211379=CARTESIAN_POINT('Ctrl Pts',(16.0189820756719,18.3356945672447,0.0424483701591674));
#211380=CARTESIAN_POINT('Ctrl Pts',(16.5291381343926,21.0253906167311,0.169624176840601));
#211381=CARTESIAN_POINT('Ctrl Pts',(19.065875791,22.0444183413159,0.296799983522036));
#211382=CARTESIAN_POINT('Ctrl Pts',(21.2962359728301,20.4669656763903,0.42397579020347));
#211383=CARTESIAN_POINT('Ctrl Pts',(21.1768856283234,17.7356987913358,0.551151596884905));
#211384=CARTESIAN_POINT('Ctrl Pts',(18.8158303252349,16.3587285734324,0.678327403566338));
#211385=CARTESIAN_POINT('Ctrl Pts',(16.3799648594531,17.5981257224815,0.805503210247773));
#211386=CARTESIAN_POINT('Ctrl Pts',(16.1036434964602,20.3174500578439,0.932679016929206));
#211387=CARTESIAN_POINT('Ctrl Pts',(18.2405820741981,22.0215634996219,1.05985482361064));
#211388=CARTESIAN_POINT('Ctrl Pts',(20.8301640752336,21.1472173052792,1.18703063029207));
#211389=CARTESIAN_POINT('Ctrl Pts',(21.4966647872182,18.4964818468598,1.31420643697351));
#211390=CARTESIAN_POINT('Ctrl Pts',(19.6285820913403,16.501288045487,1.44138224365494));
#211391=CARTESIAN_POINT('Ctrl Pts',(16.9397810066015,16.992078683811,1.56855805033638));
#211392=CARTESIAN_POINT('Ctrl Pts',(15.8970618110187,19.518596108525,1.69573385701782));
#211393=CARTESIAN_POINT('Ctrl Pts',(17.4570587119471,21.7629110154817,1.82290966369925));
#211394=CARTESIAN_POINT('Ctrl Pts',(20.1885692683029,21.6660070863072,1.95008547038068));
#211395=CARTESIAN_POINT('Ctrl Pts',(21.5856031755938,19.3167859434159,2.07726127706212));
#211396=CARTESIAN_POINT('Ctrl Pts',(20.3664679657325,16.8705130678377,2.20443708374355));
#211397=CARTESIAN_POINT('Ctrl Pts',(17.64964482037,16.5714915274638,2.33161289042498));
#211398=CARTESIAN_POINT('Ctrl Pts',(15.927650197406,18.6940552662862,2.45878869710642));
#211399=CARTESIAN_POINT('Ctrl Pts',(16.780307363717,21.2908836705225,2.58596450378785));
#211400=CARTESIAN_POINT('Ctrl Pts',(19.4253562499103,21.979547921279,2.71314031046929));
#211401=CARTESIAN_POINT('Ctrl Pts',(21.4361286945186,20.128241278265,2.84031611715073));
#211402=CARTESIAN_POINT('Ctrl Pts',(20.9678657711395,17.4354226988042,2.96749192383215));
#211403=CARTESIAN_POINT('Ctrl Pts',(18.4501696540519,16.3715860853484,3.0946677305136));
#211404=CARTESIAN_POINT('Ctrl Pts',(16.1928702618537,17.9127355062838,3.22184353719502));
#211405=CARTESIAN_POINT('Ctrl Pts',(16.2668996846349,20.6449620199907,3.34901934387646));
#211406=CARTESIAN_POINT('Ctrl Pts',(18.6043405209739,22.0616173825078,3.47619515055789));
#211407=CARTESIAN_POINT('Ctrl Pts',(21.0607358818871,20.8630082256189,3.60337095723933));
#211408=CARTESIAN_POINT('Ctrl Pts',(21.3824954846104,18.1487840570351,3.73054676392076));
#211409=CARTESIAN_POINT('Ctrl Pts',(19.2744248644109,16.4090770875045,3.8577225706022));
#211410=CARTESIAN_POINT('Ctrl Pts',(16.6705479736444,17.2399604832709,3.98489837728363));
#211411=CARTESIAN_POINT('Ctrl Pts',(15.9597602447928,19.8791502991104,4.11207418396507));
#211412=CARTESIAN_POINT('Ctrl Pts',(17.7941653025999,21.9053536856092,4.23924999064649));
#211413=CARTESIAN_POINT('Ctrl Pts',(20.4908103625543,21.4596547960069,4.36642579732794));
#211414=CARTESIAN_POINT('Ctrl Pts',(21.5756909548122,18.9509546983274,4.49360160400936));
#211415=CARTESIAN_POINT('Ctrl Pts',(20.0534964712626,16.6808300246996,4.62077741069081));
#211416=CARTESIAN_POINT('Ctrl Pts',(17.3207458725165,16.7319792633511,4.74795321737223));
#211417=CARTESIAN_POINT('Ctrl Pts',(15.8845682192929,19.0574761624978,4.87512902405368));
#211418=CARTESIAN_POINT('Ctrl Pts',(17.062567369186,21.5238216537891,5.0023048307351));
#211419=CARTESIAN_POINT('Ctrl Pts',(19.7740022170421,21.86829682763,5.12948063741654));
#211420=CARTESIAN_POINT('Ctrl Pts',(21.5312995805795,19.7748670925622,5.25665644409798));
#211421=CARTESIAN_POINT('Ctrl Pts',(20.7222481989278,17.1641242976074,5.3838322507794));
#211422=CARTESIAN_POINT('Ctrl Pts',(18.0891024993605,16.4312629161638,5.51100805746085));
#211423=CARTESIAN_POINT('Ctrl Pts',(16.0476102297768,18.2486377791988,5.63818386414227));
#211424=CARTESIAN_POINT('Ctrl Pts',(16.4707138382194,20.948920248883,5.76535967082371));
#211425=CARTESIAN_POINT('Ctrl Pts',(18.9702420247138,22.0547687577129,5.89253547750515));
#211426=CARTESIAN_POINT('Ctrl Pts',(21.253032816367,20.5516359355363,6.01971128418657));
#211427=CARTESIAN_POINT('Ctrl Pts',(21.2247673478128,17.8185528517555,6.14688709086802));
#211428=CARTESIAN_POINT('Ctrl Pts',(18.911377432097,16.3629536014721,6.27406289754945));
#211429=CARTESIAN_POINT('Ctrl Pts',(16.4352547317172,17.5202601521426,6.40123870423088));
#211430=CARTESIAN_POINT('Ctrl Pts',(16.0680881387646,20.2287155740725,6.52841451091232));
#211431=CARTESIAN_POINT('Ctrl Pts',(18.1467302133443,22.003480123343,6.65559031759375));
#211432=CARTESIAN_POINT('Ctrl Pts',(20.7641558671069,21.2163174803099,6.78276612427519));
#211433=CARTESIAN_POINT('Ctrl Pts',(21.5190395184827,18.5894005131322,6.90994193095662));
#211434=CARTESIAN_POINT('Ctrl Pts',(19.718822270698,16.5327624943404,7.03711773763806));
#211435=CARTESIAN_POINT('Ctrl Pts',(17.0150917145117,16.9332411568245,7.16429354431949));
#211436=CARTESIAN_POINT('Ctrl Pts',(15.8883528227805,19.4234221842643,7.29146935100092));
#211437=CARTESIAN_POINT('Ctrl Pts',(17.3723185953652,21.7187190420494,7.41864515768236));
#211438=CARTESIAN_POINT('Ctrl Pts',(20.1055425412228,21.7133393253515,7.54582096436379));
#211439=CARTESIAN_POINT('Ctrl Pts',(21.5804613330392,19.4122185903382,7.67299677104523));
#211440=CARTESIAN_POINT('Ctrl Pts',(20.4439285231071,16.9264922877238,7.80017257772666));
#211441=CARTESIAN_POINT('Ctrl Pts',(17.7386424233577,16.5366600185829,7.9273483844081));
#211442=CARTESIAN_POINT('Ctrl Pts',(15.946535121319,18.600368694133,8.05452419108952));
#211443=CARTESIAN_POINT('Ctrl Pts',(16.7117538358879,21.2242936927628,8.18169999777097));
#211444=CARTESIAN_POINT('Ctrl Pts',(19.3322578912771,22.0011466873821,8.30887580445239));
#211445=CARTESIAN_POINT('Ctrl Pts',(21.4038974634922,20.2182132723624,8.43605161113384));
#211446=CARTESIAN_POINT('Ctrl Pts',(21.0260718254785,17.5112241946562,8.56322741781526));
#211447=CARTESIAN_POINT('Ctrl Pts',(18.5454125496099,16.3636739183683,8.69040322449671));
#211448=CARTESIAN_POINT('Ctrl Pts',(16.237770554417,17.82836859699,8.81757903117813));
#211449=CARTESIAN_POINT('Ctrl Pts',(16.2202641420738,20.5615417720903,8.94475483785957));
#211450=CARTESIAN_POINT('Ctrl Pts',(18.5089543593347,22.0556766953737,9.071930644541));
#211451=CARTESIAN_POINT('Ctrl Pts',(21.0041099839982,20.9399973111998,9.19910645122244));
#211452=CARTESIAN_POINT('Ctrl Pts',(21.4165805972594,18.2380702076759,9.32628225790388));
#211453=CARTESIAN_POINT('Ctrl Pts',(19.3679500122646,16.4287458017761,9.4534580645853));
#211454=CARTESIAN_POINT('Ctrl Pts',(16.7377096383923,17.1719669365758,9.58063387126675));
#211455=CARTESIAN_POINT('Ctrl Pts',(15.9389417675414,19.7858743504024,9.70780967794817));
#211456=CARTESIAN_POINT('Ctrl Pts',(17.7044663440924,21.8723702284609,9.83498548462961));
#211457=CARTESIAN_POINT('Ctrl Pts',(20.4145241498733,21.5172241051722,9.96216129131105));
#211458=CARTESIAN_POINT('Ctrl Pts',(21.5828053532376,19.0462605057991,10.0893370979925));
#211459=CARTESIAN_POINT('Ctrl Pts',(20.1374844618078,16.7264351674692,10.2165129046739));
#211460=CARTESIAN_POINT('Ctrl Pts',(17.4045536867392,16.6860438535011,10.3436887113554));
#211461=CARTESIAN_POINT('Ctrl Pts',(15.8913073893432,18.9621430874931,10.4708645180368));
#211462=CARTESIAN_POINT('Ctrl Pts',(16.986055124823,21.4665530929081,10.5980403247182));
#211463=CARTESIAN_POINT('Ctrl Pts',(19.6844337935833,21.9016331309934,10.7252161313997));
#211464=CARTESIAN_POINT('Ctrl Pts',(21.5108484473051,19.8682242709185,10.8523919380811));
#211465=CARTESIAN_POINT('Ctrl Pts',(20.7896770012766,17.2318529342145,10.9795677447625));
#211466=CARTESIAN_POINT('Ctrl Pts',(18.182549496281,16.4112261906481,11.106743551444));
#211467=CARTESIAN_POINT('Ctrl Pts',(16.0813436015692,18.1592181436015,11.2339193581254));
#211468=CARTESIAN_POINT('Ctrl Pts',(16.4137853099934,20.8721546688561,11.3610951648069));
#211469=CARTESIAN_POINT('Ctrl Pts',(18.8748799877338,22.0610848883219,11.4882709714883));
#211470=CARTESIAN_POINT('Ctrl Pts',(21.2067260207266,20.6352391189707,11.6154467781697));
#211471=CARTESIAN_POINT('Ctrl Pts',(21.2699994043883,17.902742356213,11.7426225848512));
#211472=CARTESIAN_POINT('Ctrl Pts',(19.0066507363984,16.3704907820029,11.8697983915326));
#211473=CARTESIAN_POINT('Ctrl Pts',(16.4931619403762,17.4442301134199,11.996974198214));
#211474=CARTESIAN_POINT('Ctrl Pts',(16.0355029819632,20.1388711576679,12.1241500048955));
#211475=CARTESIAN_POINT('Ctrl Pts',(18.053547549985,21.9822480049345,12.2513258115769));
#211476=CARTESIAN_POINT('Ctrl Pts',(20.6958650072534,21.2831768107233,12.3785016182583));
#211477=CARTESIAN_POINT('Ctrl Pts',(21.5382930874419,18.6830120064713,12.5056774249398));
#211478=CARTESIAN_POINT('Ctrl Pts',(19.807956313961,16.5672434156512,12.6328532316212));
#211479=CARTESIAN_POINT('Ctrl Pts',(17.0923312796673,16.8769574009315,12.7600290383026));
#211480=CARTESIAN_POINT('Ctrl Pts',(15.8828354028266,19.3280106038356,12.8872048449841));
#211481=CARTESIAN_POINT('Ctrl Pts',(17.2891060806598,21.6717138402177,13.0143806516655));
#211482=CARTESIAN_POINT('Ctrl Pts',(20.0209772492569,21.7578648573255,13.1415564583469));
#211483=CARTESIAN_POINT('Ctrl Pts',(21.5721266704775,19.507425444098,13.2687322650284));
#211484=CARTESIAN_POINT('Ctrl Pts',(20.5194710255427,16.9850340841485,13.3959080717098));
#211485=CARTESIAN_POINT('Ctrl Pts',(17.8287565335022,16.5048282929666,13.5230838783912));
#211486=CARTESIAN_POINT('Ctrl Pts',(15.9685467362274,18.5073670790289,13.6502596850727));
#211487=CARTESIAN_POINT('Ctrl Pts',(16.6454686650766,21.1554453976977,13.7774354917541));
#211488=CARTESIAN_POINT('Ctrl Pts',(19.2384884648439,22.0196157498711,13.9046112984355));
#211489=CARTESIAN_POINT('Ctrl Pts',(21.3686714102025,20.3070554738911,14.031787105117));
#211490=CARTESIAN_POINT('Ctrl Pts',(21.0817068628502,17.5889323294909,14.1589629117984));
#211491=CARTESIAN_POINT('Ctrl Pts',(18.6408669839544,16.3589555959089,14.2861387184799));
#211492=CARTESIAN_POINT('Ctrl Pts',(16.2854708667935,17.7455525852409,14.4133145251613));
#211493=CARTESIAN_POINT('Ctrl Pts',(16.1764482564922,20.4766066216898,14.5404903318427));
#211494=CARTESIAN_POINT('Ctrl Pts',(18.4138206312956,22.0465451351444,14.6676661385241));
#211495=CARTESIAN_POINT('Ctrl Pts',(20.9449377043124,21.0150469808834,14.7948419452056));
#211496=CARTESIAN_POINT('Ctrl Pts',(21.4476566598927,18.3284476934456,14.922017751887));
#211497=CARTESIAN_POINT('Ctrl Pts',(19.4607640585489,16.4515353698976,15.0491935585684));
#211498=CARTESIAN_POINT('Ctrl Pts',(16.8071105415512,17.1062605727777,15.1763693652499));
#211499=CARTESIAN_POINT('Ctrl Pts',(15.9212585064325,19.6919535652726,15.3035451719313));
#211500=CARTESIAN_POINT('Ctrl Pts',(17.615922213236,21.8364015129747,15.4307209786127));
#211501=CARTESIAN_POINT('Ctrl Pts',(20.3363528936617,21.5722065233178,15.5578967852942));
#211502=CARTESIAN_POINT('Ctrl Pts',(21.5867242473895,19.1417511015219,15.6850725919756));
#211503=CARTESIAN_POINT('Ctrl Pts',(20.2198981641729,16.7748272460081,15.8122483986571));
#211504=CARTESIAN_POINT('Ctrl Pts',(17.4898527405687,16.642940686348,15.9394242053385));
#211505=CARTESIAN_POINT('Ctrl Pts',(15.9012352070049,18.8670891552265,16.0666000120199));
#211506=CARTESIAN_POINT('Ctrl Pts',(16.9115035498021,21.4067544786704,16.1937758187014));
#211507=CARTESIAN_POINT('Ctrl Pts',(19.5937992687688,21.931951351827,16.3209516253828));
#211508=CARTESIAN_POINT('Ctrl Pts',(21.4872825238012,19.9608442409695,16.4481274320642));
#211509=CARTESIAN_POINT('Ctrl Pts',(20.854799951232,17.3018015796049,16.5753032387457));
#211510=CARTESIAN_POINT('Ctrl Pts',(18.2766150550976,16.3943299707347,16.7024790454271));
#211511=CARTESIAN_POINT('Ctrl Pts',(16.1180524573998,18.0709782914572,16.8296548521085));
#211512=CARTESIAN_POINT('Ctrl Pts',(16.3594593660219,20.7935257720403,16.9568306587899));
#211513=CARTESIAN_POINT('Ctrl Pts',(18.7793599257057,22.0642040794035,17.0840064654714));
#211514=CARTESIAN_POINT('Ctrl Pts',(21.1576455689089,20.717244733731,17.2111822721528));
#211515=CARTESIAN_POINT('Ctrl Pts',(21.3123868310473,17.9883993329521,17.3383580788343));
#211516=CARTESIAN_POINT('Ctrl Pts',(19.1016182084348,16.3812141610339,17.4655338855157));
#211517=CARTESIAN_POINT('Ctrl Pts',(16.5535826965425,17.3701818600505,17.5927096921971));
#211518=CARTESIAN_POINT('Ctrl Pts',(16.0059447286121,20.0479859484101,17.7198854988786));
#211519=CARTESIAN_POINT('Ctrl Pts',(17.9611281499736,21.9579073783129,17.84706130556));
#211520=CARTESIAN_POINT('Ctrl Pts',(20.6253735238976,21.3477117809083,17.9742371122414));
#211521=CARTESIAN_POINT('Ctrl Pts',(21.5544010815252,18.7772157438201,18.1014129189229));
#211522=CARTESIAN_POINT('Ctrl Pts',(19.8958857006878,16.6046898380703,18.2285887256043));
#211523=CARTESIAN_POINT('Ctrl Pts',(17.1714123042272,16.8232917400757,18.3557645322858));
#211524=CARTESIAN_POINT('Ctrl Pts',(15.8805161335109,19.2324677726021,18.4829403389672));
#211525=CARTESIAN_POINT('Ctrl Pts',(17.2075143031097,21.6219484563438,18.6101161456486));
#211526=CARTESIAN_POINT('Ctrl Pts',(19.9349683552291,21.7995335714625,18.7372919523301));
#211527=CARTESIAN_POINT('Ctrl Pts',(21.5606084819066,19.6022997977881,18.8644677590115));
#211528=CARTESIAN_POINT('Ctrl Pts',(20.5930107655851,17.0460727454631,18.9916435656929));
#211529=CARTESIAN_POINT('Ctrl Pts',(17.919886054979,16.4760320805331,19.1188193723744));
#211530=CARTESIAN_POINT('Ctrl Pts',(15.9936603594759,18.4151547268051,19.2459951790558));
#211531=CARTESIAN_POINT('Ctrl Pts',(16.5815261991922,21.0844160225493,19.3731709857372));
#211532=CARTESIAN_POINT('Ctrl Pts',(19.1441531541393,22.0349343813413,19.5003467924186));
#211533=CARTESIAN_POINT('Ctrl Pts',(21.3304900460201,20.3946682445481,19.6275225991001));
#211534=CARTESIAN_POINT('Ctrl Pts',(21.1347084791815,17.6684599097052,19.7546984057815));
#211535=CARTESIAN_POINT('Ctrl Pts',(18.7364258833105,16.3574364640233,19.8818742124629));
#211536=CARTESIAN_POINT('Ctrl Pts',(16.3359176980786,17.6643802632539,20.0090500191444));
#211537=CARTESIAN_POINT('Ctrl Pts',(16.1355011676512,20.3902520376885,20.1362258258258));
#211538=CARTESIAN_POINT('Ctrl Pts',(18.3190460646205,22.0342325649128,20.2634016325072));
#211539=CARTESIAN_POINT('Ctrl Pts',(20.8832853850366,21.0880737832455,20.3905774391887));
#211540=CARTESIAN_POINT('Ctrl Pts',(21.4756888748341,18.4198137277981,20.5177532458701));
#211541=CARTESIAN_POINT('Ctrl Pts',(19.5527627775141,16.4774229462598,20.6449290525516));
#211542=CARTESIAN_POINT('Ctrl Pts',(16.8786730601742,17.0429098579489,20.772104859233));
#211543=CARTESIAN_POINT('Ctrl Pts',(15.9067298650559,19.5975033862937,20.8992806659144));
#211544=CARTESIAN_POINT('Ctrl Pts',(17.5286330619216,21.7974684377538,21.0264564725959));
#211545=CARTESIAN_POINT('Ctrl Pts',(20.2563826753269,21.6245778537434,21.1536322792773));
#211546=CARTESIAN_POINT('Ctrl Pts',(21.5874463311991,19.2372471517761,21.2808080859587));
#211547=CARTESIAN_POINT('Ctrl Pts',(20.300639179667,16.8260911603011,21.4079838926401));
#211548=CARTESIAN_POINT('Ctrl Pts',(17.5765588401915,16.6024498642087,21.5351596993216));
#211549=CARTESIAN_POINT('Ctrl Pts',(15.9143183086354,18.7729382233993,21.662335506003));
#211550=CARTESIAN_POINT('Ctrl Pts',(16.8390399827,21.3434932755793,21.7895113126845));
#211551=CARTESIAN_POINT('Ctrl Pts',(19.5021077373455,21.9611708420245,21.9166871193659));
#211552=CARTESIAN_POINT('Ctrl Pts',(21.4611725520066,20.0483226159722,22.0438815838219));
#211553=CARTESIAN_POINT('Ctrl Pts',(21.097729963592,18.2714051422367,22.1286841127175));
#211554=CARTESIAN_POINT('Ctrl Pts',(20.5799309194189,17.6565535467265,22.1710947060526));
#211555=CARTESIAN_POINT('Ctrl Pts',(18.1489776472236,17.0246983287242,-0.171345836529519));
#211556=CARTESIAN_POINT('Ctrl Pts',(17.4210583805961,17.2194788787227,-0.128953900969041));
#211557=CARTESIAN_POINT('Ctrl Pts',(16.1877700772709,18.3901108027545,-0.0441700298480844));
#211558=CARTESIAN_POINT('Ctrl Pts',(16.6662106099602,20.9125930681132,0.0830057768333494));
#211559=CARTESIAN_POINT('Ctrl Pts',(19.0452436430351,21.8682695891329,0.210181583514784));
#211560=CARTESIAN_POINT('Ctrl Pts',(21.1369461627689,20.3888844472776,0.337357390196218));
#211561=CARTESIAN_POINT('Ctrl Pts',(21.0250156242086,17.8274157338044,0.464533196877653));
#211562=CARTESIAN_POINT('Ctrl Pts',(18.81074307445,16.5360493895473,0.591709003559087));
#211563=CARTESIAN_POINT('Ctrl Pts',(16.5263111813342,17.6983953463737,0.718884810240521));
#211564=CARTESIAN_POINT('Ctrl Pts',(16.2671682429258,20.2486639579588,0.846060616921955));
#211565=CARTESIAN_POINT('Ctrl Pts',(18.271257019252,21.8468355936962,0.973236423603391));
#211566=CARTESIAN_POINT('Ctrl Pts',(20.6998491546166,21.0268460006587,1.10041223028482));
#211567=CARTESIAN_POINT('Ctrl Pts',(21.3249146619818,18.5409022133311,1.22758803696626));
#211568=CARTESIAN_POINT('Ctrl Pts',(19.5729674590718,16.669746184055,1.35476384364769));
#211569=CARTESIAN_POINT('Ctrl Pts',(17.0513245200395,17.1300252112755,1.48193965032912));
#211570=CARTESIAN_POINT('Ctrl Pts',(16.073429386086,19.4994733867219,1.60911545701056));
#211571=CARTESIAN_POINT('Ctrl Pts',(17.5364439588135,21.6042630902867,1.73629126369199));
#211572=CARTESIAN_POINT('Ctrl Pts',(20.0981411949616,21.5133835119668,1.86346707037343));
#211573=CARTESIAN_POINT('Ctrl Pts',(21.4083239034943,19.3102094129899,1.99064287705486));
#211574=CARTESIAN_POINT('Ctrl Pts',(20.2649802358942,17.0160171208712,2.1178186837363));
#211575=CARTESIAN_POINT('Ctrl Pts',(17.7170573196222,16.7355852361245,2.24499449041773));
#211576=CARTESIAN_POINT('Ctrl Pts',(16.1021161450239,18.7261928325832,2.37217029709916));
#211577=CARTESIAN_POINT('Ctrl Pts',(16.9017650796541,21.1615808747066,2.4993461037806));
#211578=CARTESIAN_POINT('Ctrl Pts',(19.3823758191848,21.8074320517016,2.62652191046204));
#211579=CARTESIAN_POINT('Ctrl Pts',(21.2681419942009,20.0712179632603,2.75369771714347));
#211580=CARTESIAN_POINT('Ctrl Pts',(20.8289901725761,17.5458072902532,2.8808735238249));
#211581=CARTESIAN_POINT('Ctrl Pts',(18.4678148992109,16.5481075720289,3.00804933050634));
#211582=CARTESIAN_POINT('Ctrl Pts',(16.3508479335524,17.9934463802261,3.13522513718777));
#211583=CARTESIAN_POINT('Ctrl Pts',(16.420275074257,20.5558150638861,3.26240094386921));
#211584=CARTESIAN_POINT('Ctrl Pts',(18.6124012281085,21.8843993954715,3.38957675055063));
#211585=CARTESIAN_POINT('Ctrl Pts',(20.9160867080332,20.7603057113817,3.51675255723208));
#211586=CARTESIAN_POINT('Ctrl Pts',(21.2178430688434,18.2148201979656,3.64392836391351));
#211587=CARTESIAN_POINT('Ctrl Pts',(19.2408275787131,16.5832678229678,3.77110417059494));
#211588=CARTESIAN_POINT('Ctrl Pts',(16.7988292423621,17.3624966249737,3.89827997727638));
#211589=CARTESIAN_POINT('Ctrl Pts',(16.1322299659104,19.8376125424924,4.02545578395781));
#211590=CARTESIAN_POINT('Ctrl Pts',(17.8525932116705,21.7378503442426,4.15263159063924));
#211591=CARTESIAN_POINT('Ctrl Pts',(20.3815924794505,21.3198597891662,4.27980739732068));
#211592=CARTESIAN_POINT('Ctrl Pts',(21.3990279084555,18.9671212681321,4.40698320400211));
#211593=CARTESIAN_POINT('Ctrl Pts',(19.97146564174,16.8381263467644,4.53415901068355));
#211594=CARTESIAN_POINT('Ctrl Pts',(17.4086054545075,16.8860957250923,4.66133481736498));
#211595=CARTESIAN_POINT('Ctrl Pts',(16.0617124995014,19.0670204758143,4.78851062404641));
#211596=CARTESIAN_POINT('Ctrl Pts',(17.1664774653348,21.3800375035998,4.91568643072785));
#211597=CARTESIAN_POINT('Ctrl Pts',(19.7093470653026,21.7030972474828,5.04286223740928));
#211598=CARTESIAN_POINT('Ctrl Pts',(21.3573962697213,19.7398124437998,5.17003804409073));
#211599=CARTESIAN_POINT('Ctrl Pts',(20.5986422230066,17.2913750447324,5.29721385077215));
#211600=CARTESIAN_POINT('Ctrl Pts',(18.1291946694319,16.6040743967612,5.42438965745359));
#211601=CARTESIAN_POINT('Ctrl Pts',(16.214618468201,18.3084661857105,5.55156546413503));
#211602=CARTESIAN_POINT('Ctrl Pts',(16.6114184519424,20.8408767317044,5.67874127081646));
#211603=CARTESIAN_POINT('Ctrl Pts',(18.9555552637581,21.8779765379183,5.80591707749789));
#211604=CARTESIAN_POINT('Ctrl Pts',(21.0964288723461,20.4682909018246,5.93309288417933));
#211605=CARTESIAN_POINT('Ctrl Pts',(21.069920619429,17.905118899581,6.06026869086075));
#211606=CARTESIAN_POINT('Ctrl Pts',(18.9003501817706,16.5400117548499,6.1874444975422));
#211607=CARTESIAN_POINT('Ctrl Pts',(16.5781637771942,17.6253705448169,6.31462030422363));
#211608=CARTESIAN_POINT('Ctrl Pts',(16.2338233007557,20.1654459446513,6.44179611090507));
#211609=CARTESIAN_POINT('Ctrl Pts',(18.1832397674068,21.8298764298645,6.5689719175865));
#211610=CARTESIAN_POINT('Ctrl Pts',(20.637944563427,21.09165033648,6.69614772426795));
#211611=CARTESIAN_POINT('Ctrl Pts',(21.3458983946297,18.6280442856993,6.82332353094937));
#211612=CARTESIAN_POINT('Ctrl Pts',(19.657597561457,16.6992639204773,6.9504993376308));
#211613=CARTESIAN_POINT('Ctrl Pts',(17.1219532905771,17.0748455122945,7.07767514431223));
#211614=CARTESIAN_POINT('Ctrl Pts',(16.0652618206899,19.4102162618813,7.20485095099367));
#211615=CARTESIAN_POINT('Ctrl Pts',(17.4569719897474,21.5628184559476,7.3320267576751));
#211616=CARTESIAN_POINT('Ctrl Pts',(20.0202760969144,21.5577731869978,7.45920256435654));
#211617=CARTESIAN_POINT('Ctrl Pts',(21.4035017204607,19.3997091761485,7.58637837103798));
#211618=CARTESIAN_POINT('Ctrl Pts',(20.3376252034471,17.0685162087954,7.7135541777194));
#211619=CARTESIAN_POINT('Ctrl Pts',(17.8005220944761,16.7029191423313,7.84072998440084));
#211620=CARTESIAN_POINT('Ctrl Pts',(16.1198270256501,18.638330593724,7.96790579108228));
#211621=CARTESIAN_POINT('Ctrl Pts',(16.8374734069165,21.099130681503,8.09508159776372));
#211622=CARTESIAN_POINT('Ctrl Pts',(19.2950652256212,21.8276880596097,8.22225740444514));
#211623=CARTESIAN_POINT('Ctrl Pts',(21.2379145234536,20.155596553002,8.34943321112658));
#211624=CARTESIAN_POINT('Ctrl Pts',(20.8835776564797,17.616896337289,8.47660901780802));
#211625=CARTESIAN_POINT('Ctrl Pts',(18.5571367075217,16.5406872908817,8.60378482448944));
#211626=CARTESIAN_POINT('Ctrl Pts',(16.3929568520385,17.9143244167918,8.73096063117089));
#211627=CARTESIAN_POINT('Ctrl Pts',(16.3765387832853,20.4775809095323,8.85813643785231));
#211628=CARTESIAN_POINT('Ctrl Pts',(18.5229450603227,21.878828030654,8.98531224453375));
#211629=CARTESIAN_POINT('Ctrl Pts',(20.8629811449671,20.8325085177327,9.11248805121519));
#211630=CARTESIAN_POINT('Ctrl Pts',(21.2498091685766,18.2985555819606,9.23966385789662));
#211631=CARTESIAN_POINT('Ctrl Pts',(19.3285384287442,16.6017137670521,9.36683966457805));
#211632=CARTESIAN_POINT('Ctrl Pts',(16.8618155817556,17.2987301203051,9.49401547125949));
#211633=CARTESIAN_POINT('Ctrl Pts',(16.1127057376362,19.7501353993238,9.62119127794092));
#211634=CARTESIAN_POINT('Ctrl Pts',(17.7684706833649,21.7069174119797,9.74836708462235));
#211635=CARTESIAN_POINT('Ctrl Pts',(20.3100488495983,21.3738501132499,9.87554289130379));
#211636=CARTESIAN_POINT('Ctrl Pts',(21.405700016949,19.0565020772309,10.0027186979853));
#211637=CARTESIAN_POINT('Ctrl Pts',(20.0502322431535,16.8808962961301,10.1298945046667));
#211638=CARTESIAN_POINT('Ctrl Pts',(17.487203080851,16.8430160407836,10.2570703113481));
#211639=CARTESIAN_POINT('Ctrl Pts',(16.0680327069235,18.9776140943582,10.3842461180296));
#211640=CARTESIAN_POINT('Ctrl Pts',(17.0947218558021,21.3263292307962,10.511421924711));
#211641=CARTESIAN_POINT('Ctrl Pts',(19.6253469569058,21.7343610901177,10.6385977313924));
#211642=CARTESIAN_POINT('Ctrl Pts',(21.3382165482799,19.8273657667087,10.7657735380739));
#211643=CARTESIAN_POINT('Ctrl Pts',(20.6618790925152,17.3548931083184,10.8929493447553));
#211644=CARTESIAN_POINT('Ctrl Pts',(18.2168322270393,16.5852833200597,11.0201251514367));
#211645=CARTESIAN_POINT('Ctrl Pts',(16.2462546942025,18.2246056152896,11.1473009581182));
#211646=CARTESIAN_POINT('Ctrl Pts',(16.5580290725475,20.768883535951,11.2744767647995));
#211647=CARTESIAN_POINT('Ctrl Pts',(18.8661217208428,21.8839000055346,11.401652571481));
#211648=CARTESIAN_POINT('Ctrl Pts',(21.0530008906637,20.5466966189245,11.5288283781625));
#211649=CARTESIAN_POINT('Ctrl Pts',(21.1123406767285,17.984074487133,11.6560041848439));
#211650=CARTESIAN_POINT('Ctrl Pts',(18.9897005083654,16.5470803618114,11.7831799915254));
#211651=CARTESIAN_POINT('Ctrl Pts',(16.6324709941403,17.554067163028,11.9103557982068));
#211652=CARTESIAN_POINT('Ctrl Pts',(16.2032639071911,20.0811870013163,12.0375316048882));
#211653=CARTESIAN_POINT('Ctrl Pts',(18.0958501101972,21.8099642757934,12.1647074115696));
#211654=CARTESIAN_POINT('Ctrl Pts',(20.5738992290484,21.1543531371454,12.2918832182511));
#211655=CARTESIAN_POINT('Ctrl Pts',(21.3639550022726,18.7158361132654,12.4190590249325));
#211656=CARTESIAN_POINT('Ctrl Pts',(19.7411902943285,16.7316012221275,12.546234831614));
#211657=CARTESIAN_POINT('Ctrl Pts',(17.1943910046178,17.0220608208441,12.6734106382954));
#211658=CARTESIAN_POINT('Ctrl Pts',(16.0600874092589,19.3207362555485,12.8005864449768));
#211659=CARTESIAN_POINT('Ctrl Pts',(17.3789326541725,21.5187354867873,12.9277622516583));
#211660=CARTESIAN_POINT('Ctrl Pts',(19.940968083918,21.5995306431169,13.0549380583397));
#211661=CARTESIAN_POINT('Ctrl Pts',(21.3956852095567,19.4889971833178,13.1821138650211));
#211662=CARTESIAN_POINT('Ctrl Pts',(20.4084713582425,17.1234185622757,13.3092896717026));
#211663=CARTESIAN_POINT('Ctrl Pts',(17.8850339651544,16.6730663404289,13.436465478384));
#211664=CARTESIAN_POINT('Ctrl Pts',(16.1404702162623,18.5511107293104,13.5636412850654));
#211665=CARTESIAN_POINT('Ctrl Pts',(16.7753090713368,21.0345625667023,13.6908170917469));
#211666=CARTESIAN_POINT('Ctrl Pts',(19.2071252833902,21.8450089322025,13.8179928984283));
#211667=CARTESIAN_POINT('Ctrl Pts',(21.2048784133999,20.2389155874388,13.9451687051097));
#211668=CARTESIAN_POINT('Ctrl Pts',(20.9357539591253,17.6897734908367,14.0723445117912));
#211669=CARTESIAN_POINT('Ctrl Pts',(18.6466569036158,16.5362622984264,14.1995203184726));
#211670=CARTESIAN_POINT('Ctrl Pts',(16.4376917179148,17.8366569342653,14.326696125154));
#211671=CARTESIAN_POINT('Ctrl Pts',(16.3354468560612,20.3979260315651,14.4538719318355));
#211672=CARTESIAN_POINT('Ctrl Pts',(18.4337256327737,21.8702641638416,14.5810477385169));
#211673=CARTESIAN_POINT('Ctrl Pts',(20.8074875042872,20.9028924783419,14.7082235451983));
#211674=CARTESIAN_POINT('Ctrl Pts',(21.2789532857658,18.3833144546537,14.8353993518798));
#211675=CARTESIAN_POINT('Ctrl Pts',(19.4155823851695,16.6230865468621,14.9625751585612));
#211676=CARTESIAN_POINT('Ctrl Pts',(16.9269019499539,17.2371086083006,15.0897509652427));
#211677=CARTESIAN_POINT('Ctrl Pts',(16.0961218145012,19.6620535081066,15.2169267719241));
#211678=CARTESIAN_POINT('Ctrl Pts',(17.6854311890587,21.6731848097627,15.3441025786055));
#211679=CARTESIAN_POINT('Ctrl Pts',(20.2367373661345,21.425414368886,15.4712783852869));
#211680=CARTESIAN_POINT('Ctrl Pts',(21.4093752801818,19.1460561866125,15.5984541919684));
#211681=CARTESIAN_POINT('Ctrl Pts',(20.1275224271794,16.9262799222545,15.7256299986498));
#211682=CARTESIAN_POINT('Ctrl Pts',(17.5671992389961,16.8025925235073,15.8528058053313));
#211683=CARTESIAN_POINT('Ctrl Pts',(16.0773433292112,18.8884695018156,15.9799816120127));
#211684=CARTESIAN_POINT('Ctrl Pts',(17.0248050241658,21.2702481937078,16.1071574186941));
#211685=CARTESIAN_POINT('Ctrl Pts',(19.5403470248439,21.7627944792304,16.2343332253756));
#211686=CARTESIAN_POINT('Ctrl Pts',(21.3161156777683,19.9142277122867,16.361509032057));
#211687=CARTESIAN_POINT('Ctrl Pts',(20.7229534605137,17.4204931665544,16.4886848387384));
#211688=CARTESIAN_POINT('Ctrl Pts',(18.3050498916118,16.5694375091209,16.6158606454198));
#211689=CARTESIAN_POINT('Ctrl Pts',(16.2806814235098,18.1418514832104,16.7430364521013));
#211690=CARTESIAN_POINT('Ctrl Pts',(16.5070804792137,20.6951428626135,16.8702122587827));
#211691=CARTESIAN_POINT('Ctrl Pts',(18.7765399770255,21.8868252818636,16.9973880654642));
#211692=CARTESIAN_POINT('Ctrl Pts',(21.0069716862451,20.6236040854512,17.1245638721456));
#211693=CARTESIAN_POINT('Ctrl Pts',(21.1520929498682,18.0644063167351,17.251739678827));
#211694=CARTESIAN_POINT('Ctrl Pts',(19.0787640157619,16.5571370867842,17.3789154855085));
#211695=CARTESIAN_POINT('Ctrl Pts',(16.6891354956622,17.4846223624005,17.5060912921899));
#211696=CARTESIAN_POINT('Ctrl Pts',(16.1755432396875,19.9959519694325,17.6332670988714));
#211697=CARTESIAN_POINT('Ctrl Pts',(18.0091762655641,21.7871368641264,17.7604429055528));
#211698=CARTESIAN_POINT('Ctrl Pts',(20.5077900801511,21.2148760790659,17.8876187122342));
#211699=CARTESIAN_POINT('Ctrl Pts',(21.3790615900277,18.8041833660481,18.0147945189156));
#211700=CARTESIAN_POINT('Ctrl Pts',(19.8236532620919,16.7667196647752,18.1419703255971));
#211701=CARTESIAN_POINT('Ctrl Pts',(17.2685556976942,16.9717314619586,18.2691461322785));
#211702=CARTESIAN_POINT('Ctrl Pts',(16.0579123249335,19.231133158048,18.3963219389599));
#211703=CARTESIAN_POINT('Ctrl Pts',(17.3024132973075,21.4720639313621,18.5234977456414));
#211704=CARTESIAN_POINT('Ctrl Pts',(19.8603062151207,21.6386088848577,18.6506735523228));
#211705=CARTESIAN_POINT('Ctrl Pts',(21.3848830869879,19.5779733613755,18.7778493590042));
#211706=CARTESIAN_POINT('Ctrl Pts',(20.4774392589433,17.1806625548439,18.9050251656857));
#211707=CARTESIAN_POINT('Ctrl Pts',(17.9704981207863,16.6460603390679,19.0322009723671));
#211708=CARTESIAN_POINT('Ctrl Pts',(16.1640225686834,18.4646310606594,19.1593767790485));
#211709=CARTESIAN_POINT('Ctrl Pts',(16.7153417987421,20.9679489658214,19.28655258573));
#211710=CARTESIAN_POINT('Ctrl Pts',(19.1186546369411,21.8593752306623,19.4137283924114));
#211711=CARTESIAN_POINT('Ctrl Pts',(21.1690707190565,20.3210816226097,19.5409041990928));
#211712=CARTESIAN_POINT('Ctrl Pts',(20.985460555994,17.7643569779692,19.6680800057743));
#211713=CARTESIAN_POINT('Ctrl Pts',(18.7362750703113,16.5348376083611,19.7952558124557));
#211714=CARTESIAN_POINT('Ctrl Pts',(16.485002356336,17.7605309561315,19.9224316191372));
#211715=CARTESIAN_POINT('Ctrl Pts',(16.2970453774111,20.3169399637462,20.0496074258186));
#211716=CARTESIAN_POINT('Ctrl Pts',(18.3448430381436,21.8587170449558,20.1767832325));
#211717=CARTESIAN_POINT('Ctrl Pts',(20.7496680038194,20.9713793298171,20.3039590391814));
#211718=CARTESIAN_POINT('Ctrl Pts',(21.3052427860467,18.4690004195621,20.4311348458629));
#211719=CARTESIAN_POINT('Ctrl Pts',(19.5018617017747,16.6473647370611,20.5583106525443));
#211720=CARTESIAN_POINT('Ctrl Pts',(16.9940155496951,17.1776962986144,20.6854864592258));
#211721=CARTESIAN_POINT('Ctrl Pts',(16.0824963938076,19.5734751345466,20.8126622659072));
#211722=CARTESIAN_POINT('Ctrl Pts',(17.6035686543715,21.6366721369649,20.9398380725886));
#211723=CARTESIAN_POINT('Ctrl Pts',(20.1617387589333,21.4745298636412,21.0670138792701));
#211724=CARTESIAN_POINT('Ctrl Pts',(21.4100524732811,19.2356154114268,21.1941896859515));
#211725=CARTESIAN_POINT('Ctrl Pts',(20.2032439124044,16.9743568470362,21.3213654926329));
#211726=CARTESIAN_POINT('Ctrl Pts',(17.6485149693138,16.7646189462416,21.4485412993143));
#211727=CARTESIAN_POINT('Ctrl Pts',(16.0896130768821,18.8001717717257,21.5757171059958));
#211728=CARTESIAN_POINT('Ctrl Pts',(16.9568463925819,21.2109198309685,21.7028929126772));
#211729=CARTESIAN_POINT('Ctrl Pts',(19.4543557984586,21.7901974439036,21.8300687193587));
#211730=CARTESIAN_POINT('Ctrl Pts',(21.2916289180791,19.9962677069502,21.9572631838147));
#211731=CARTESIAN_POINT('Ctrl Pts',(20.950780931212,18.329818140889,22.0420657127103));
#211732=CARTESIAN_POINT('Ctrl Pts',(20.46517256435,17.753190813129,22.0844763060453));
#211733=CARTESIAN_POINT('Ctrl Pts',(18.1877584159729,17.169626909876,-0.257964236536771));
#211734=CARTESIAN_POINT('Ctrl Pts',(17.5080924658439,17.3514955780797,-0.215572300976293));
#211735=CARTESIAN_POINT('Ctrl Pts',(16.3565580788699,18.4445270382643,-0.130788429855337));
#211736=CARTESIAN_POINT('Ctrl Pts',(16.8032830855277,20.7997955194952,-0.00361262317390214));
#211737=CARTESIAN_POINT('Ctrl Pts',(19.0246114950703,21.6921208369499,0.123563183507532));
#211738=CARTESIAN_POINT('Ctrl Pts',(20.9776563527076,20.3108032181647,0.250738990188966));
#211739=CARTESIAN_POINT('Ctrl Pts',(20.8731456200936,17.9191326762732,0.377914796870401));
#211740=CARTESIAN_POINT('Ctrl Pts',(18.8056558236651,16.7133702056622,0.505090603551835));
#211741=CARTESIAN_POINT('Ctrl Pts',(16.6726575032154,17.7986649702659,0.632266410233269));
#211742=CARTESIAN_POINT('Ctrl Pts',(16.4306929893915,20.1798778580737,0.759442216914703));
#211743=CARTESIAN_POINT('Ctrl Pts',(18.301931964306,21.6721076877706,0.886618023596138));
#211744=CARTESIAN_POINT('Ctrl Pts',(20.5695342339997,20.9064746960381,1.01379383027758));
#211745=CARTESIAN_POINT('Ctrl Pts',(21.1531645367453,18.5853225798024,1.14096963695901));
#211746=CARTESIAN_POINT('Ctrl Pts',(19.5173528268034,16.8382043226231,1.26814544364044));
#211747=CARTESIAN_POINT('Ctrl Pts',(17.1628680334775,17.2679717387401,1.39532125032188));
#211748=CARTESIAN_POINT('Ctrl Pts',(16.2497969611534,19.4803506649187,1.52249705700331));
#211749=CARTESIAN_POINT('Ctrl Pts',(17.6158292056801,21.4456151650917,1.64967286368475));
#211750=CARTESIAN_POINT('Ctrl Pts',(20.0077131216202,21.3607599376264,1.77684867036618));
#211751=CARTESIAN_POINT('Ctrl Pts',(21.2310446313948,19.3036328825639,1.90402447704762));
#211752=CARTESIAN_POINT('Ctrl Pts',(20.1634925060559,17.1615211739047,2.03120028372905));
#211753=CARTESIAN_POINT('Ctrl Pts',(17.7844698188743,16.8996789447851,2.15837609041049));
#211754=CARTESIAN_POINT('Ctrl Pts',(16.2765820926419,18.7583303988802,2.28555189709192));
#211755=CARTESIAN_POINT('Ctrl Pts',(17.0232227955911,21.0322780788906,2.41272770377336));
#211756=CARTESIAN_POINT('Ctrl Pts',(19.3393953884592,21.6353161821242,2.53990351045478));
#211757=CARTESIAN_POINT('Ctrl Pts',(21.1001552938832,20.0141946482555,2.66707931713622));
#211758=CARTESIAN_POINT('Ctrl Pts',(20.6901145740129,17.6561918817021,2.79425512381766));
#211759=CARTESIAN_POINT('Ctrl Pts',(18.4854601443698,16.7246290587094,2.92143093049909));
#211760=CARTESIAN_POINT('Ctrl Pts',(16.5088256052511,18.0741572541683,3.04860673718052));
#211761=CARTESIAN_POINT('Ctrl Pts',(16.5736504638791,20.4666681077815,3.17578254386197));
#211762=CARTESIAN_POINT('Ctrl Pts',(18.6204619352431,21.7071814084352,3.30295835054339));
#211763=CARTESIAN_POINT('Ctrl Pts',(20.7714375341794,20.6576031971447,3.43013415722483));
#211764=CARTESIAN_POINT('Ctrl Pts',(21.0531906530764,18.2808563388961,3.55730996390626));
#211765=CARTESIAN_POINT('Ctrl Pts',(19.2072302930153,16.7574585584311,3.6844857705877));
#211766=CARTESIAN_POINT('Ctrl Pts',(16.9271105110797,17.4850327666767,3.81166157726913));
#211767=CARTESIAN_POINT('Ctrl Pts',(16.3046996870279,19.7960747858742,3.93883738395057));
#211768=CARTESIAN_POINT('Ctrl Pts',(17.911021120741,21.5703470028761,4.066013190632));
#211769=CARTESIAN_POINT('Ctrl Pts',(20.2723745963467,21.1800647823256,4.19318899731344));
#211770=CARTESIAN_POINT('Ctrl Pts',(21.2223648620988,18.9832878379367,4.32036480399487));
#211771=CARTESIAN_POINT('Ctrl Pts',(19.8894348122174,16.9954226688293,4.44754061067631));
#211772=CARTESIAN_POINT('Ctrl Pts',(17.4964650364985,17.0402121868336,4.57471641735773));
#211773=CARTESIAN_POINT('Ctrl Pts',(16.23885677971,19.0765647891309,4.70189222403917));
#211774=CARTESIAN_POINT('Ctrl Pts',(17.2703875614835,21.2362533534106,4.8290680307206));
#211775=CARTESIAN_POINT('Ctrl Pts',(19.6446919135629,21.5378976673356,4.95624383740204));
#211776=CARTESIAN_POINT('Ctrl Pts',(21.1834929588632,19.7047577950374,5.08341964408348));
#211777=CARTESIAN_POINT('Ctrl Pts',(20.4750362470855,17.4186257918574,5.21059545076491));
#211778=CARTESIAN_POINT('Ctrl Pts',(18.1692868395033,16.7768858773585,5.33777125744635));
#211779=CARTESIAN_POINT('Ctrl Pts',(16.3816267066251,18.3682945922223,5.46494706412778));
#211780=CARTESIAN_POINT('Ctrl Pts',(16.7521230656655,20.7328332145257,5.59212287080921));
#211781=CARTESIAN_POINT('Ctrl Pts',(18.9408685028023,21.7011843181237,5.71929867749065));
#211782=CARTESIAN_POINT('Ctrl Pts',(20.9398249283253,20.3849458681128,5.84647448417208));
#211783=CARTESIAN_POINT('Ctrl Pts',(20.9150738910453,17.9916849474066,5.97365029085351));
#211784=CARTESIAN_POINT('Ctrl Pts',(18.889322931444,16.7170699082275,6.10082609753496));
#211785=CARTESIAN_POINT('Ctrl Pts',(16.7210728226713,17.7304809374911,6.22800190421637));
#211786=CARTESIAN_POINT('Ctrl Pts',(16.3995584627467,20.1021763152302,6.35517771089783));
#211787=CARTESIAN_POINT('Ctrl Pts',(18.2197493214694,21.6562727363857,6.48235351757925));
#211788=CARTESIAN_POINT('Ctrl Pts',(20.5117332597471,20.96698319265,6.6095293242607));
#211789=CARTESIAN_POINT('Ctrl Pts',(21.1727572707768,18.6666880582664,6.73670513094212));
#211790=CARTESIAN_POINT('Ctrl Pts',(19.5963728522159,16.8657653466142,6.86388093762356));
#211791=CARTESIAN_POINT('Ctrl Pts',(17.2288148666425,17.2164498677646,6.99105674430498));
#211792=CARTESIAN_POINT('Ctrl Pts',(16.2421708185993,19.3970103394982,7.11823255098643));
#211793=CARTESIAN_POINT('Ctrl Pts',(17.5416253841297,21.406917869846,7.24540835766785));
#211794=CARTESIAN_POINT('Ctrl Pts',(19.935009652606,21.4022070486441,7.3725841643493));
#211795=CARTESIAN_POINT('Ctrl Pts',(21.2265421078823,19.3871997619589,7.49975997103072));
#211796=CARTESIAN_POINT('Ctrl Pts',(20.2313218837872,17.210540129867,7.62693577771217));
#211797=CARTESIAN_POINT('Ctrl Pts',(17.8624017655944,16.8691782660797,7.75411158439359));
#211798=CARTESIAN_POINT('Ctrl Pts',(16.2931189299813,18.676292493315,7.88128739107503));
#211799=CARTESIAN_POINT('Ctrl Pts',(16.9631929779452,20.9739676702432,8.00846319775646));
#211800=CARTESIAN_POINT('Ctrl Pts',(19.2578725599652,21.6542294318373,8.13563900443789));
#211801=CARTESIAN_POINT('Ctrl Pts',(21.0719315834152,20.0929798336416,8.26281481111933));
#211802=CARTESIAN_POINT('Ctrl Pts',(20.7410834874809,17.7225684799219,8.38999061780077));
#211803=CARTESIAN_POINT('Ctrl Pts',(18.5688608654335,16.7177006633949,8.5171664244822));
#211804=CARTESIAN_POINT('Ctrl Pts',(16.5481431496601,18.0002802365935,8.64434223116363));
#211805=CARTESIAN_POINT('Ctrl Pts',(16.5328134244968,20.3936200469742,8.77151803784506));
#211806=CARTESIAN_POINT('Ctrl Pts',(18.5369357613108,21.7019793659344,8.89869384452652));
#211807=CARTESIAN_POINT('Ctrl Pts',(20.721852305936,20.7250197242656,9.02586965120793));
#211808=CARTESIAN_POINT('Ctrl Pts',(21.0830377398936,18.3590409562453,9.15304545788938));
#211809=CARTESIAN_POINT('Ctrl Pts',(19.2891268452239,16.774681732328,9.2802212645708));
#211810=CARTESIAN_POINT('Ctrl Pts',(16.985921525119,17.4254933040343,9.40739707125225));
#211811=CARTESIAN_POINT('Ctrl Pts',(16.2864697077309,19.7143964482452,9.53457287793367));
#211812=CARTESIAN_POINT('Ctrl Pts',(17.8324750226373,21.5414645954985,9.66174868461511));
#211813=CARTESIAN_POINT('Ctrl Pts',(20.2055735493235,21.2304761213276,9.78892449129655));
#211814=CARTESIAN_POINT('Ctrl Pts',(21.2285946806605,19.0667436486627,9.91610029797797));
#211815=CARTESIAN_POINT('Ctrl Pts',(19.9629800244992,17.0353574247909,10.0432761046594));
#211816=CARTESIAN_POINT('Ctrl Pts',(17.5698524749629,16.999988228066,10.1704519113408));
#211817=CARTESIAN_POINT('Ctrl Pts',(16.2447580245038,18.9930851012233,10.2976277180222));
#211818=CARTESIAN_POINT('Ctrl Pts',(17.2033885867812,21.1861053686842,10.4248035247037));
#211819=CARTESIAN_POINT('Ctrl Pts',(19.5662601202284,21.567089049242,10.5519793313851));
#211820=CARTESIAN_POINT('Ctrl Pts',(21.1655846492548,19.786507262499,10.6791551380666));
#211821=CARTESIAN_POINT('Ctrl Pts',(20.534081183754,17.4779332824223,10.806330944748));
#211822=CARTESIAN_POINT('Ctrl Pts',(18.2511149577974,16.7593404494715,10.9335067514294));
#211823=CARTESIAN_POINT('Ctrl Pts',(16.4111657868359,18.2899930869776,11.0606825581108));
#211824=CARTESIAN_POINT('Ctrl Pts',(16.7022728351016,20.6656124030459,11.1878583647923));
#211825=CARTESIAN_POINT('Ctrl Pts',(18.8573634539519,21.7067151227473,11.3150341714737));
#211826=CARTESIAN_POINT('Ctrl Pts',(20.8992757606008,20.4581541188783,11.4422099781552));
#211827=CARTESIAN_POINT('Ctrl Pts',(20.9546819490687,18.065406618053,11.5693857848366));
#211828=CARTESIAN_POINT('Ctrl Pts',(18.9727502803322,16.7236699416198,11.696561591518));
#211829=CARTESIAN_POINT('Ctrl Pts',(16.7717800479045,17.663904212636,11.8237373981994));
#211830=CARTESIAN_POINT('Ctrl Pts',(16.371024832419,20.0235028449647,11.9509132048809));
#211831=CARTESIAN_POINT('Ctrl Pts',(18.1381526704095,21.6376805466522,12.0780890115623));
#211832=CARTESIAN_POINT('Ctrl Pts',(20.4519334508432,21.0255294635675,12.2052648182438));
#211833=CARTESIAN_POINT('Ctrl Pts',(21.1896169171035,18.7486602200595,12.3324406249252));
#211834=CARTESIAN_POINT('Ctrl Pts',(19.6744242746961,16.8959590286039,12.4596164316066));
#211835=CARTESIAN_POINT('Ctrl Pts',(17.2964507295683,17.1671642407565,12.5867922382881));
#211836=CARTESIAN_POINT('Ctrl Pts',(16.2373394156911,19.3134619072614,12.7139680449695));
#211837=CARTESIAN_POINT('Ctrl Pts',(17.4687592276853,21.365757133357,12.8411438516509));
#211838=CARTESIAN_POINT('Ctrl Pts',(19.8609589185792,21.4411964289083,12.9683196583324));
#211839=CARTESIAN_POINT('Ctrl Pts',(21.2192437486358,19.4705689225376,13.0954954650138));
#211840=CARTESIAN_POINT('Ctrl Pts',(20.2974716909424,17.2618030404029,13.2226712716952));
#211841=CARTESIAN_POINT('Ctrl Pts',(17.9413113968065,16.8413043878911,13.3498470783767));
#211842=CARTESIAN_POINT('Ctrl Pts',(16.3123936962972,18.5948543795921,13.4770228850581));
#211843=CARTESIAN_POINT('Ctrl Pts',(16.9051494775971,20.9136797357071,13.6041986917395));
#211844=CARTESIAN_POINT('Ctrl Pts',(19.1757621019364,21.6704021145338,13.731374498421));
#211845=CARTESIAN_POINT('Ctrl Pts',(21.0410854165974,20.1707757009864,13.8585503051024));
#211846=CARTESIAN_POINT('Ctrl Pts',(20.7898010554004,17.7906146521824,13.9857261117838));
#211847=CARTESIAN_POINT('Ctrl Pts',(18.6524468232773,16.7135690009438,14.1129019184653));
#211848=CARTESIAN_POINT('Ctrl Pts',(16.5899125690362,17.9277612832899,14.2400777251467));
#211849=CARTESIAN_POINT('Ctrl Pts',(16.4944454556301,20.3192454414403,14.3672535318281));
#211850=CARTESIAN_POINT('Ctrl Pts',(18.4536306342518,21.6939831925389,14.4944293385096));
#211851=CARTESIAN_POINT('Ctrl Pts',(20.670037304262,20.7907379758005,14.621605145191));
#211852=CARTESIAN_POINT('Ctrl Pts',(21.1102499116389,18.438181215862,14.7487809518724));
#211853=CARTESIAN_POINT('Ctrl Pts',(19.37040071179,16.7946377238266,14.8759567585539));
#211854=CARTESIAN_POINT('Ctrl Pts',(17.0466933583566,17.3679566438234,15.0031325652353));
#211855=CARTESIAN_POINT('Ctrl Pts',(16.27098512257,19.6321534509405,15.1303083719167));
#211856=CARTESIAN_POINT('Ctrl Pts',(17.7549401648813,21.5099681065509,15.2574841785982));
#211857=CARTESIAN_POINT('Ctrl Pts',(20.1371218386074,21.278622214454,15.3846599852796));
#211858=CARTESIAN_POINT('Ctrl Pts',(21.2320263129741,19.1503612717033,15.5118357919611));
#211859=CARTESIAN_POINT('Ctrl Pts',(20.0351466901858,17.0777325985008,15.6390115986425));
#211860=CARTESIAN_POINT('Ctrl Pts',(17.6445457374235,16.9622443606664,15.7661874053239));
#211861=CARTESIAN_POINT('Ctrl Pts',(16.2534514514175,18.9098498484046,15.8933632120053));
#211862=CARTESIAN_POINT('Ctrl Pts',(17.1381064985295,21.1337419087451,16.0205390186868));
#211863=CARTESIAN_POINT('Ctrl Pts',(19.4868947809189,21.5936376066338,16.1477148253682));
#211864=CARTESIAN_POINT('Ctrl Pts',(21.1449488317356,19.8676111836039,16.2748906320497));
#211865=CARTESIAN_POINT('Ctrl Pts',(20.5911069697954,17.5391847535037,16.4020664387311));
#211866=CARTESIAN_POINT('Ctrl Pts',(18.3334847281261,16.7445450475071,16.5292422454125));
#211867=CARTESIAN_POINT('Ctrl Pts',(16.4433103896197,18.2127246749636,16.656418052094));
#211868=CARTESIAN_POINT('Ctrl Pts',(16.6547015924054,20.5967599531865,16.7835938587754));
#211869=CARTESIAN_POINT('Ctrl Pts',(18.7737200283452,21.7094464843237,16.9107696654568));
#211870=CARTESIAN_POINT('Ctrl Pts',(20.8562978035812,20.5299634371713,17.0379454721383));
#211871=CARTESIAN_POINT('Ctrl Pts',(20.9917990686889,18.140413300518,17.1651212788197));
#211872=CARTESIAN_POINT('Ctrl Pts',(19.0559098230889,16.7330600125345,17.2922970855011));
#211873=CARTESIAN_POINT('Ctrl Pts',(16.8246882947818,17.5990628647505,17.4194728921826));
#211874=CARTESIAN_POINT('Ctrl Pts',(16.3451417507631,19.9439179904547,17.546648698864));
#211875=CARTESIAN_POINT('Ctrl Pts',(18.0572243811545,21.6163663499399,17.6738245055454));
#211876=CARTESIAN_POINT('Ctrl Pts',(20.3902066364046,21.0820403772236,17.8010003122269));
#211877=CARTESIAN_POINT('Ctrl Pts',(21.2037220985302,18.8311509882762,17.9281761189083));
#211878=CARTESIAN_POINT('Ctrl Pts',(19.7514208234961,16.92874949148,18.0553519255897));
#211879=CARTESIAN_POINT('Ctrl Pts',(17.3656990911611,17.1201711838414,18.1825277322712));
#211880=CARTESIAN_POINT('Ctrl Pts',(16.2353085163561,19.229798543494,18.3097035389526));
#211881=CARTESIAN_POINT('Ctrl Pts',(17.3973122915052,21.3221794063805,18.4368793456341));
#211882=CARTESIAN_POINT('Ctrl Pts',(19.7856440750124,21.4776841982527,18.5640551523154));
#211883=CARTESIAN_POINT('Ctrl Pts',(21.2091576920692,19.5536469249632,18.6912309589969));
#211884=CARTESIAN_POINT('Ctrl Pts',(20.3618677523014,17.3152523642247,18.8184067656783));
#211885=CARTESIAN_POINT('Ctrl Pts',(18.0211101865936,16.8160885976028,18.9455825723598));
#211886=CARTESIAN_POINT('Ctrl Pts',(16.3343847778911,18.5141073945138,19.0727583790412));
#211887=CARTESIAN_POINT('Ctrl Pts',(16.849157398292,20.8514819090936,19.1999341857227));
#211888=CARTESIAN_POINT('Ctrl Pts',(19.093156119743,21.6838160799832,19.327109992404));
#211889=CARTESIAN_POINT('Ctrl Pts',(21.0076513920927,20.2474950006713,19.4542857990855));
#211890=CARTESIAN_POINT('Ctrl Pts',(20.8362126328065,17.8602540462332,19.5814616057669));
#211891=CARTESIAN_POINT('Ctrl Pts',(18.7361242573121,16.7122387526989,19.7086374124484));
#211892=CARTESIAN_POINT('Ctrl Pts',(16.6340870145935,17.8566816490089,19.8358132191298));
#211893=CARTESIAN_POINT('Ctrl Pts',(16.4585895871711,20.243627889804,19.9629890258113));
#211894=CARTESIAN_POINT('Ctrl Pts',(18.3706400116666,21.6832015249988,20.0901648324927));
#211895=CARTESIAN_POINT('Ctrl Pts',(20.6160506226023,20.8546848763886,20.2173406391741));
#211896=CARTESIAN_POINT('Ctrl Pts',(21.1347966972592,18.518187111326,20.3445164458556));
#211897=CARTESIAN_POINT('Ctrl Pts',(19.4509606260352,16.8173065278623,20.471692252537));
#211898=CARTESIAN_POINT('Ctrl Pts',(17.1093580392161,17.31248273928,20.5988680592184));
#211899=CARTESIAN_POINT('Ctrl Pts',(16.2582629225594,19.5494468827994,20.7260438658998));
#211900=CARTESIAN_POINT('Ctrl Pts',(17.6785042468215,21.475875836176,20.8532196725813));
#211901=CARTESIAN_POINT('Ctrl Pts',(20.0670948425395,21.324481873539,20.9803954792627));
#211902=CARTESIAN_POINT('Ctrl Pts',(21.2326586153631,19.2339836710777,21.1075712859442));
#211903=CARTESIAN_POINT('Ctrl Pts',(20.1058486451417,17.1226225337713,21.2347470926256));
#211904=CARTESIAN_POINT('Ctrl Pts',(17.7204710984363,16.9267880282744,21.361922899307));
#211905=CARTESIAN_POINT('Ctrl Pts',(16.2649078451288,18.8274053200522,21.4890987059885));
#211906=CARTESIAN_POINT('Ctrl Pts',(17.0746528024638,21.0783463863576,21.6162745126699));
#211907=CARTESIAN_POINT('Ctrl Pts',(19.4066038595716,21.6192240457828,21.7434503193513));
#211908=CARTESIAN_POINT('Ctrl Pts',(21.1220852841517,19.9442127979284,21.8706447838074));
#211909=CARTESIAN_POINT('Ctrl Pts',(20.803831898832,18.3882311395412,21.955447312703));
#211910=CARTESIAN_POINT('Ctrl Pts',(20.3504142092811,17.8498280795315,21.997857906038));
#211911=CARTESIAN_POINT('Ctrl Pts',(18.0722627314315,16.7380050975816,-1.38821246165044E-15));
#211912=CARTESIAN_POINT('Ctrl Pts',(17.9906109534297,16.7675693131061,3.14657425492808E-14));
#211913=CARTESIAN_POINT('Ctrl Pts',(17.9108508876399,16.801533969706,-6.59917533869226E-15));
#211914=CARTESIAN_POINT('Ctrl Pts',(17.833184560489,16.8395812357412,-8.91647866652079E-16));
#211915=CARTESIAN_POINT('Ctrl Pts',(17.753672918109,16.878532486837,4.95148776083561E-15));
#211916=CARTESIAN_POINT('Ctrl Pts',(17.6763549684744,16.9217633043155,1.81124826743322E-14));
#211917=CARTESIAN_POINT('Ctrl Pts',(17.6014769244535,16.9689790985685,1.02903796594944E-14));
#211918=CARTESIAN_POINT('Ctrl Pts',(17.5314114952628,17.0131602057565,2.97102440556189E-15));
#211919=CARTESIAN_POINT('Ctrl Pts',(17.4634822740683,17.0608314720463,-1.12028222644949E-14));
#211920=CARTESIAN_POINT('Ctrl Pts',(17.3979218193959,17.1117790406503,-1.23859256184744E-14));
#211921=CARTESIAN_POINT('Ctrl Pts',(17.3682534093495,17.1348346061396,-1.26972994741572E-14));
#211922=CARTESIAN_POINT('Ctrl Pts',(17.3390705414607,17.1585614233309,-2.36992619559033E-14));
#211923=CARTESIAN_POINT('Ctrl Pts',(17.310397157226,17.1829409553506,-2.57363574895919E-14));
#211924=CARTESIAN_POINT('Ctrl Pts',(17.2926919353297,17.1979948122865,-2.73746264744599E-14));
#211925=CARTESIAN_POINT('Ctrl Pts',(17.27518100039,17.2132975506653,-1.30461038077809E-14));
#211926=CARTESIAN_POINT('Ctrl Pts',(17.257870302469,17.2288449191993,8.43075609324728E-15));
#211927=CARTESIAN_POINT('Ctrl Pts',(17.2457082697189,17.239768083947,2.37421180105107E-14));
#211928=CARTESIAN_POINT('Ctrl Pts',(17.2336433007629,17.2508137998582,1.24222163529167E-14));
#211929=CARTESIAN_POINT('Ctrl Pts',(17.2216943574194,17.2619645032884,7.13318293321663E-15));
#211930=CARTESIAN_POINT('Ctrl Pts',(17.1582625823413,17.3211587677194,-2.04006785318585E-14));
#211931=CARTESIAN_POINT('Ctrl Pts',(17.0979931462804,17.3834003799274,-7.07776241633133E-15));
#211932=CARTESIAN_POINT('Ctrl Pts',(17.041116608508,17.4484111431914,-9.93649607039515E-15));
#211933=CARTESIAN_POINT('Ctrl Pts',(16.9849624648484,17.5125961987999,-1.27589206866276E-14));
#211934=CARTESIAN_POINT('Ctrl Pts',(16.9321151284134,17.5794813469652,-1.13917247600207E-14));
#211935=CARTESIAN_POINT('Ctrl Pts',(16.8828390026439,17.6488249957205,-1.36696209906972E-14));
#211936=CARTESIAN_POINT('Ctrl Pts',(16.8374017786414,17.7127663639275,-1.57700556265627E-14));
#211937=CARTESIAN_POINT('Ctrl Pts',(16.7950011366575,17.7787988087824,4.9988445844417E-15));
#211938=CARTESIAN_POINT('Ctrl Pts',(16.7558820673411,17.8467441370846,-6.6197047843275E-15));
#211939=CARTESIAN_POINT('Ctrl Pts',(16.7395100185488,17.8751805045547,-1.13588888870035E-14));
#211940=CARTESIAN_POINT('Ctrl Pts',(16.723713229623,17.903952012734,1.05054445318429E-15));
#211941=CARTESIAN_POINT('Ctrl Pts',(16.7085117731593,17.9330458325382,-3.71924713249427E-15));
#211942=CARTESIAN_POINT('Ctrl Pts',(16.6986550833365,17.9519103905663,-6.78822109791206E-15));
#211943=CARTESIAN_POINT('Ctrl Pts',(16.6890487140929,17.9709104592438,-1.73998603743695E-14));
#211944=CARTESIAN_POINT('Ctrl Pts',(16.6796984374459,17.9900425446149,-6.07847105982273E-15));
#211945=CARTESIAN_POINT('Ctrl Pts',(16.6737724856049,18.0021679416281,5.77327818760497E-16));
#211946=CARTESIAN_POINT('Ctrl Pts',(16.6679532270762,18.0143385914813,-2.27240940409281E-16));
#211947=CARTESIAN_POINT('Ctrl Pts',(16.6622433304787,18.0265499321002,-2.60902410786912E-15));
#211948=CARTESIAN_POINT('Ctrl Pts',(16.6271177976284,18.1016703548131,-1.76610440863303E-14));
#211949=CARTESIAN_POINT('Ctrl Pts',(16.5961057017263,18.1783725156421,1.14199974843153E-14));
#211950=CARTESIAN_POINT('Ctrl Pts',(16.5694538401813,18.2564278430498,-4.413136522885E-15));
#211951=CARTESIAN_POINT('Ctrl Pts',(16.5428019786364,18.3344831704575,-2.02462705300853E-14));
#211952=CARTESIAN_POINT('Ctrl Pts',(16.5205098793409,18.4138923942319,-1.04020717721636E-14));
#211953=CARTESIAN_POINT('Ctrl Pts',(16.5028786483266,18.4944362051925,-9.4091401336982E-15));
#211954=CARTESIAN_POINT('Ctrl Pts',(16.4850464602744,18.5758980374565,-8.6237439592604E-15));
#211955=CARTESIAN_POINT('Ctrl Pts',(16.4719827280125,18.6585216956155,2.62324771514716E-14));
#211956=CARTESIAN_POINT('Ctrl Pts',(16.4636117053936,18.7419152200439,1.9373391779709E-14));
#211957=CARTESIAN_POINT('Ctrl Pts',(16.4601585345833,18.7763162839797,1.65439174766097E-14));
#211958=CARTESIAN_POINT('Ctrl Pts',(16.4575045102803,18.8108481987005,1.22831063379818E-14));
#211959=CARTESIAN_POINT('Ctrl Pts',(16.4556467292437,18.845482524778,3.83026943495679E-15));
#211960=CARTESIAN_POINT('Ctrl Pts',(16.454914769638,18.859128335107,7.25867713128221E-16));
#211961=CARTESIAN_POINT('Ctrl Pts',(16.4543064277075,18.8727920340357,1.66417253216955E-14));
#211962=CARTESIAN_POINT('Ctrl Pts',(16.4538219965805,18.8864542247022,1.65978342181461E-14));
#211963=CARTESIAN_POINT('Ctrl Pts',(16.4509322011605,18.9679538101119,1.63150992925569E-14));
#211964=CARTESIAN_POINT('Ctrl Pts',(16.4524389841394,19.0495303086149,-1.1559845979381E-14));
#211965=CARTESIAN_POINT('Ctrl Pts',(16.458209072107,19.1308246613079,-1.14352971536391E-14));
#211966=CARTESIAN_POINT('Ctrl Pts',(16.4640075078912,19.2125184043422,-1.13101364330193E-14));
#211967=CARTESIAN_POINT('Ctrl Pts',(16.4741116098947,19.2939282562812,4.47511337812399E-16));
#211968=CARTESIAN_POINT('Ctrl Pts',(16.488437388537,19.3746780989798,9.6034291630076E-15));
#211969=CARTESIAN_POINT('Ctrl Pts',(16.5025242207701,19.4540810770198,1.86066311224743E-14));
#211970=CARTESIAN_POINT('Ctrl Pts',(16.5206935647305,19.5328467549076,-9.24683669832954E-15));
#211971=CARTESIAN_POINT('Ctrl Pts',(16.5429083611786,19.6105921329423,-6.10622663543836E-15));
#211972=CARTESIAN_POINT('Ctrl Pts',(16.5522119867793,19.6431521382123,-4.79092940769646E-15));
#211973=CARTESIAN_POINT('Ctrl Pts',(16.5622256486959,19.6755328027629,-3.85337688317397E-15));
#211974=CARTESIAN_POINT('Ctrl Pts',(16.5729486044555,19.7077040845634,-4.63518112781003E-15));
#211975=CARTESIAN_POINT('Ctrl Pts',(16.5784892728338,19.7243273373082,-5.02631740729074E-15));
#211976=CARTESIAN_POINT('Ctrl Pts',(16.5842201982241,19.7408967187103,7.50369055471448E-15));
#211977=CARTESIAN_POINT('Ctrl Pts',(16.59013339505,19.757386717525,3.58046925441613E-15));
#211978=CARTESIAN_POINT('Ctrl Pts',(16.6171691937068,19.8327808403536,-1.42609449952302E-14));
#211979=CARTESIAN_POINT('Ctrl Pts',(16.6480432448069,19.9066161661436,-5.97332593345049E-15));
#211980=CARTESIAN_POINT('Ctrl Pts',(16.6826949054327,19.9785209088995,4.21884749357559E-15));
#211981=CARTESIAN_POINT('Ctrl Pts',(16.708683650902,20.0324494659664,1.17631662849405E-14));
#211982=CARTESIAN_POINT('Ctrl Pts',(16.7367982565916,20.085291634914,-2.01726906480219E-14));
#211983=CARTESIAN_POINT('Ctrl Pts',(16.7670276708943,20.1368764988564,-7.7715611723761E-15));
#211984=CARTESIAN_POINT('Ctrl Pts',(16.776261941294,20.1526342828943,-4.1977974750146E-15));
#211985=CARTESIAN_POINT('Ctrl Pts',(16.7856936339531,20.1682746431805,1.04387754400567E-14));
#211986=CARTESIAN_POINT('Ctrl Pts',(16.7953226427023,20.1837924294014,1.13797860024079E-15));
#211987=CARTESIAN_POINT('Ctrl Pts',(16.803547563051,20.1970474340419,-6.69839811468132E-15));
#211988=CARTESIAN_POINT('Ctrl Pts',(16.8119141832479,20.2102092393014,2.41113709074752E-14));
#211989=CARTESIAN_POINT('Ctrl Pts',(16.8204178931759,20.2232683327282,1.87905246917808E-14));
#211990=CARTESIAN_POINT('Ctrl Pts',(16.8615694216389,20.2864644741072,-6.83040447856231E-15));
#211991=CARTESIAN_POINT('Ctrl Pts',(16.9059580723631,20.3473056667748,-2.18788826067377E-15));
#211992=CARTESIAN_POINT('Ctrl Pts',(16.9535504700224,20.4054521814502,4.52415882534751E-15));
#211993=CARTESIAN_POINT('Ctrl Pts',(16.997682676699,20.459371171234,1.18644907122736E-14));
#211994=CARTESIAN_POINT('Ctrl Pts',(17.0445702571952,20.51097318916,3.05264786508281E-14));
#211995=CARTESIAN_POINT('Ctrl Pts',(17.0942091691994,20.55995417271,1.27675647831893E-14));
#211996=CARTESIAN_POINT('Ctrl Pts',(17.0997977295932,20.5654686607127,1.06142302750383E-14));
#211997=CARTESIAN_POINT('Ctrl Pts',(17.1054211843278,20.5709498884042,1.6560443839516E-15));
#211998=CARTESIAN_POINT('Ctrl Pts',(17.1110791648801,20.5763977067475,3.95239396766556E-14));
#211999=CARTESIAN_POINT('Ctrl Pts',(20.3504145393176,-17.5908279157877,
0.00214189257971319));
#212000=CARTESIAN_POINT('Ctrl Pts',(20.8038322616566,-18.1292310654914,
0.0445524841607406));
#212001=CARTESIAN_POINT('Ctrl Pts',(21.1220877448274,-19.685210814566,0.129355011302246));
#212002=CARTESIAN_POINT('Ctrl Pts',(19.4066026967562,-21.3602255324577,
0.25654947400423));
#212003=CARTESIAN_POINT('Ctrl Pts',(17.0746532893504,-20.819345744412,0.383725280685664));
#212004=CARTESIAN_POINT('Ctrl Pts',(16.264907281043,-18.5684058059804,0.510901087367099));
#212005=CARTESIAN_POINT('Ctrl Pts',(17.7204711810805,-16.6677874925037,
0.638076894048533));
#212006=CARTESIAN_POINT('Ctrl Pts',(20.105848679288,-16.8636225373773,0.765252700729967));
#212007=CARTESIAN_POINT('Ctrl Pts',(21.2326588952387,-18.9749835563125,
0.892428507411401));
#212008=CARTESIAN_POINT('Ctrl Pts',(20.0670949402048,-21.0654821373604,
1.01960431409284));
#212009=CARTESIAN_POINT('Ctrl Pts',(17.678504162672,-21.2168760062151,1.14678012077427));
#212010=CARTESIAN_POINT('Ctrl Pts',(16.2582626864848,-19.2904469366441,
1.2739559274557));
#212011=CARTESIAN_POINT('Ctrl Pts',(17.1093578926688,-17.0534825509078,
1.40113173413714));
#212012=CARTESIAN_POINT('Ctrl Pts',(19.4509606903938,-16.5583063136444,
1.52830754081857));
#212013=CARTESIAN_POINT('Ctrl Pts',(21.1347969203461,-18.2591870432273,
1.65548334750001));
#212014=CARTESIAN_POINT('Ctrl Pts',(20.6160507961411,-20.5956850306546,
1.78265915418144));
#212015=CARTESIAN_POINT('Ctrl Pts',(18.3706399783416,-21.4242017524251,
1.90983496086288));
#212016=CARTESIAN_POINT('Ctrl Pts',(16.4585893765604,-19.9846279859987,
2.03701076754431));
#212017=CARTESIAN_POINT('Ctrl Pts',(16.6340868204421,-17.5976815233674,
2.16418657422575));
#212018=CARTESIAN_POINT('Ctrl Pts',(18.7361242574674,-16.453238521784,2.29136238090717));
#212019=CARTESIAN_POINT('Ctrl Pts',(20.8362128272701,-17.6012539211848,
2.41853818758862));
#212020=CARTESIAN_POINT('Ctrl Pts',(21.0076516023807,-19.9884950966021,
2.54571399427004));
#212021=CARTESIAN_POINT('Ctrl Pts',(19.0931561529689,-21.4248163086708,
2.67288980095148));
#212022=CARTESIAN_POINT('Ctrl Pts',(16.8491572239522,-20.5924820608467,
2.80006560763291));
#212023=CARTESIAN_POINT('Ctrl Pts',(16.3343845559425,-18.2551073300457,
2.92724141431435));
#212024=CARTESIAN_POINT('Ctrl Pts',(18.0211101206545,-16.557088376093,3.05441722099578));
#212025=CARTESIAN_POINT('Ctrl Pts',(20.3618679028699,-17.0562521888763,
3.18159302767722));
#212026=CARTESIAN_POINT('Ctrl Pts',(21.2091579210064,-19.2946469566574,
3.30876883435865));
#212027=CARTESIAN_POINT('Ctrl Pts',(19.7856441722836,-21.2186844079067,
3.43594464104009));
#212028=CARTESIAN_POINT('Ctrl Pts',(17.3973121678696,-21.0631796016525,
3.56312044772152));
#212029=CARTESIAN_POINT('Ctrl Pts',(16.2353082852419,-18.9707985452326,
3.69029625440296));
#212030=CARTESIAN_POINT('Ctrl Pts',(17.3656989646013,-16.8611709904523,
3.81747206108439));
#212031=CARTESIAN_POINT('Ctrl Pts',(19.7514209176014,-16.6697492803852,
3.94464786776582));
#212032=CARTESIAN_POINT('Ctrl Pts',(21.2037223269647,-18.5721509531424,
4.07182367444726));
#212033=CARTESIAN_POINT('Ctrl Pts',(20.390206789594,-20.8230405502836,4.19899948112869));
#212034=CARTESIAN_POINT('Ctrl Pts',(18.0572243185569,-21.357366572422,4.32617528781012));
#212035=CARTESIAN_POINT('Ctrl Pts',(16.3451415298078,-19.6849180582454,
4.45335109449157));
#212036=CARTESIAN_POINT('Ctrl Pts',(16.8246881181817,-17.340062715656,4.58052690117299));
#212037=CARTESIAN_POINT('Ctrl Pts',(19.0559098528636,-16.4740597833398,
4.70770270785444));
#212038=CARTESIAN_POINT('Ctrl Pts',(20.9917992775219,-17.8814132014949,
4.83487851453586));
#212039=CARTESIAN_POINT('Ctrl Pts',(20.8562979998813,-20.2709635591674,
4.9620543212173));
#212040=CARTESIAN_POINT('Ctrl Pts',(18.7737200320192,-21.4504467154151,
5.08923012789874));
#212041=CARTESIAN_POINT('Ctrl Pts',(16.6547014000827,-20.3377600813612,
5.21640593458017));
#212042=CARTESIAN_POINT('Ctrl Pts',(16.4433101777445,-17.9537245826292,
5.34358174126161));
#212043=CARTESIAN_POINT('Ctrl Pts',(18.3334846910807,-16.4855448193747,
5.47075754794303));
#212044=CARTESIAN_POINT('Ctrl Pts',(20.5911071415668,-17.2801845988706,
5.59793335462448));
#212045=CARTESIAN_POINT('Ctrl Pts',(21.144949054734,-19.6086112443364,5.7251091613059));
#212046=CARTESIAN_POINT('Ctrl Pts',(19.4868948505574,-21.3346378270135,
5.85228496798734));
#212047=CARTESIAN_POINT('Ctrl Pts',(17.1381063509189,-20.8747420865874,
5.97946077466877));
#212048=CARTESIAN_POINT('Ctrl Pts',(16.2534512219814,-18.6508498205501,
6.10663658135021));
#212049=CARTESIAN_POINT('Ctrl Pts',(17.6445456366553,-16.7032441526699,
6.23381238803165));
#212050=CARTESIAN_POINT('Ctrl Pts',(20.0351468105341,-16.8187324011862,
6.36098819471307));
#212051=CARTESIAN_POINT('Ctrl Pts',(21.2320265440266,-18.8913612660945,
6.48816400139451));
#212052=CARTESIAN_POINT('Ctrl Pts',(20.137121968388,-21.0196224056966,6.61533980807595));
#212053=CARTESIAN_POINT('Ctrl Pts',(17.7549400743242,-21.2509683191918,
6.74251561475738));
#212054=CARTESIAN_POINT('Ctrl Pts',(16.2709848947557,-19.3731534898947,
6.86969142143882));
#212055=CARTESIAN_POINT('Ctrl Pts',(17.0466932022907,-17.1089564733528,
6.99686722812024));
#212056=CARTESIAN_POINT('Ctrl Pts',(19.3704007706532,-16.5356375003274,
7.12404303480169));
#212057=CARTESIAN_POINT('Ctrl Pts',(21.1102501314279,-18.1791811443807,
7.25121884148312));
#212058=CARTESIAN_POINT('Ctrl Pts',(20.6700374833341,-20.5317381219169,
7.37839464816456));
#212059=CARTESIAN_POINT('Ctrl Pts',(18.4536306083194,-21.4349834222001,
7.50557045484598));
#212060=CARTESIAN_POINT('Ctrl Pts',(16.4944452484847,-20.0602455439464,
7.63274626152742));
#212061=CARTESIAN_POINT('Ctrl Pts',(16.5899123707208,-17.668761164598,7.75992206820886));
#212062=CARTESIAN_POINT('Ctrl Pts',(18.652446815734,-16.4545687699462,7.88709787489029));
#212063=CARTESIAN_POINT('Ctrl Pts',(20.7898012455497,-17.531614520805,8.01427368157173));
#212064=CARTESIAN_POINT('Ctrl Pts',(21.0410856299891,-19.9117757897599,
8.14144948825315));
#212065=CARTESIAN_POINT('Ctrl Pts',(19.175762142797,-21.4114023420139,8.2686252949346));
#212066=CARTESIAN_POINT('Ctrl Pts',(16.9051493084394,-20.6546798931949,
8.39580110161602));
#212067=CARTESIAN_POINT('Ctrl Pts',(16.312393472313,-18.3358543226023,8.52297690829747));
#212068=CARTESIAN_POINT('Ctrl Pts',(17.9413113234874,-16.5823041687085,
8.65015271497889));
#212069=CARTESIAN_POINT('Ctrl Pts',(20.2974718355542,-17.0028028601137,
8.77732852166035));
#212070=CARTESIAN_POINT('Ctrl Pts',(21.2192439785061,-19.2115689465461,
8.90450432834176));
#212071=CARTESIAN_POINT('Ctrl Pts',(19.8609590228163,-21.1821966351882,
9.0316801350232));
#212072=CARTESIAN_POINT('Ctrl Pts',(17.4687591106581,-21.1067573326593,
9.15885594170464));
#212073=CARTESIAN_POINT('Ctrl Pts',(16.2373391847649,-19.0544619167386,
9.28603174838607));
#212074=CARTESIAN_POINT('Ctrl Pts',(17.2964505966034,-16.908164051714,9.4132075550675));
#212075=CARTESIAN_POINT('Ctrl Pts',(19.6744243616797,-16.6369588144763,
9.54038336174894));
#212076=CARTESIAN_POINT('Ctrl Pts',(21.1896171442334,-18.4896601772957,
9.66755916843036));
#212077=CARTESIAN_POINT('Ctrl Pts',(20.4519336097419,-20.7665296314006,
9.79473497511182));
#212078=CARTESIAN_POINT('Ctrl Pts',(18.1381526152972,-21.3786807711059,
9.92191078179324));
#212079=CARTESIAN_POINT('Ctrl Pts',(16.3710246138578,-19.7645029201165,
10.0490865884747));
#212080=CARTESIAN_POINT('Ctrl Pts',(16.7717798664108,-17.4049040695389,
10.1762623951561));
#212081=CARTESIAN_POINT('Ctrl Pts',(18.9727503024152,-16.4646697115565,
10.3034382018376));
#212082=CARTESIAN_POINT('Ctrl Pts',(20.9546821544686,-17.8064065120923,
10.430614008519));
#212083=CARTESIAN_POINT('Ctrl Pts',(20.8992759608759,-20.1991542342326,
10.5577898152005));
#212084=CARTESIAN_POINT('Ctrl Pts',(18.8573634653625,-21.4477153535862,
10.6849656218819));
#212085=CARTESIAN_POINT('Ctrl Pts',(16.702272647179,-20.4066125375889,10.8121414285633));
#212086=CARTESIAN_POINT('Ctrl Pts',(16.4111655719875,-18.0309930017901,
10.9393172352448));
#212087=CARTESIAN_POINT('Ctrl Pts',(18.2511149131334,-16.5003402227076,
11.0664930419262));
#212088=CARTESIAN_POINT('Ctrl Pts',(20.5340813502507,-17.2189331221239,
11.1936688486076));
#212089=CARTESIAN_POINT('Ctrl Pts',(21.165584874162,-19.5275073157298,11.3208446552891));
#212090=CARTESIAN_POINT('Ctrl Pts',(19.5662601972076,-21.3080892671662,
11.4480204619705));
#212091=CARTESIAN_POINT('Ctrl Pts',(17.2033884452088,-20.9271055513698,
11.575196268652));
#212092=CARTESIAN_POINT('Ctrl Pts',(16.2447577942638,-18.7340850810675,
11.7023720753333));
#212093=CARTESIAN_POINT('Ctrl Pts',(17.5698523672862,-16.7409880235606,
11.8295478820148));
#212094=CARTESIAN_POINT('Ctrl Pts',(19.9629801381724,-16.7763572235568,
11.9567236886962));
#212095=CARTESIAN_POINT('Ctrl Pts',(21.2285949113957,-18.8077436353198,
12.0838994953777));
#212096=CARTESIAN_POINT('Ctrl Pts',(20.2055736854352,-20.9714763081171,
12.2110753020591));
#212097=CARTESIAN_POINT('Ctrl Pts',(17.8324749392518,-21.2824648110527,
12.3382511087405));
#212098=CARTESIAN_POINT('Ctrl Pts',(16.2864694813489,-19.4553964948066,
12.465426915422));
#212099=CARTESIAN_POINT('Ctrl Pts',(16.9859213634321,-17.1664931388855,
12.5926027221034));
#212100=CARTESIAN_POINT('Ctrl Pts',(19.2891268965698,-16.515681506983,12.7197785287849));
#212101=CARTESIAN_POINT('Ctrl Pts',(21.0830379571657,-18.100040877444,12.8469543354662));
#212102=CARTESIAN_POINT('Ctrl Pts',(20.7218524898006,-20.4660198643034,
12.9741301421477));
#212103=CARTESIAN_POINT('Ctrl Pts',(18.5369357430837,-21.4429795963352,
13.1013059488291));
#212104=CARTESIAN_POINT('Ctrl Pts',(16.5328132209002,-20.1346201563596,
13.2284817555106));
#212105=CARTESIAN_POINT('Ctrl Pts',(16.5481429474813,-17.7412801246093,
13.355657562192));
#212106=CARTESIAN_POINT('Ctrl Pts',(18.5688608501589,-16.4587004327796,
13.4828333688734));
#212107=CARTESIAN_POINT('Ctrl Pts',(20.7410836731242,-17.4635683422508,
13.6100091755549));
#212108=CARTESIAN_POINT('Ctrl Pts',(21.0719317996599,-19.8339799152194,
13.7371849822363));
#212109=CARTESIAN_POINT('Ctrl Pts',(19.2578726084204,-21.3952296578215,
13.8643607889177));
#212110=CARTESIAN_POINT('Ctrl Pts',(16.9631928141561,-20.7149678333072,
13.9915365955992));
#212111=CARTESIAN_POINT('Ctrl Pts',(16.2931187042143,-18.4172924438578,
14.1187124022806));
#212112=CARTESIAN_POINT('Ctrl Pts',(17.8624016849767,-16.6101780494751,
14.245888208962));
#212113=CARTESIAN_POINT('Ctrl Pts',(20.2313220222805,-16.9515399448363,
14.3730640156435));
#212114=CARTESIAN_POINT('Ctrl Pts',(21.2265423384276,-19.1281997782562,
14.5002398223249));
#212115=CARTESIAN_POINT('Ctrl Pts',(19.9350097636923,-21.1432072513177,
14.6274156290064));
#212116=CARTESIAN_POINT('Ctrl Pts',(17.5416252738421,-21.1479180729553,
14.7545914356878));
#212117=CARTESIAN_POINT('Ctrl Pts',(16.2421705881198,-19.1380103567032,
14.8817672423692));
#212118=CARTESIAN_POINT('Ctrl Pts',(17.2288147274218,-16.9574496832805,
15.0089430490507));
#212119=CARTESIAN_POINT('Ctrl Pts',(19.5963729319801,-16.6067651296939,
15.1361188557321));
#212120=CARTESIAN_POINT('Ctrl Pts',(21.1727574963474,-18.4076880079207,
15.2632946624135));
#212121=CARTESIAN_POINT('Ctrl Pts',(20.511733424177,-20.707983355068,15.3904704690949));
#212122=CARTESIAN_POINT('Ctrl Pts',(18.2197492739044,-21.397272962559,15.5176462757764));
#212123=CARTESIAN_POINT('Ctrl Pts',(16.3995582468247,-19.8431763976587,
15.6448220824578));
#212124=CARTESIAN_POINT('Ctrl Pts',(16.7210726364874,-17.471480800552,15.7719978891392));
#212125=CARTESIAN_POINT('Ctrl Pts',(18.8893229458104,-16.4580696775538,
15.8991736958207));
#212126=CARTESIAN_POINT('Ctrl Pts',(20.9150740927816,-17.732684834627,16.0263495025021));
#212127=CARTESIAN_POINT('Ctrl Pts',(20.939825132351,-20.1259459766957,16.1535253091836));
#212128=CARTESIAN_POINT('Ctrl Pts',(18.9408685219365,-21.4421845484509,
16.280701115865));
#212129=CARTESIAN_POINT('Ctrl Pts',(16.7521228823537,-20.4738333552863,
16.4078769225464));
#212130=CARTESIAN_POINT('Ctrl Pts',(16.3816264890446,-18.1092945142772,
16.5350527292279));
#212131=CARTESIAN_POINT('Ctrl Pts',(18.1692867872707,-16.5178856522175,
16.6622285359093));
#212132=CARTESIAN_POINT('Ctrl Pts',(20.475036408121,-17.1596256260734,16.7894043425907));
#212133=CARTESIAN_POINT('Ctrl Pts',(21.1834931854267,-19.445757840707,16.9165801492722));
#212134=CARTESIAN_POINT('Ctrl Pts',(19.6446919977966,-21.2788978825597,
17.0437559559536));
#212135=CARTESIAN_POINT('Ctrl Pts',(17.2703874261082,-20.9772535407345,
17.1709317626351));
#212136=CARTESIAN_POINT('Ctrl Pts',(16.2388565489241,-18.8175647766965,
17.2981075693165));
#212137=CARTESIAN_POINT('Ctrl Pts',(17.4964649220338,-16.7812119860487,
17.4252833759979));
#212138=CARTESIAN_POINT('Ctrl Pts',(19.8894349190882,-16.7364224639015,
17.5524591826793));
#212139=CARTESIAN_POINT('Ctrl Pts',(21.2223650922577,-18.7242878168747,
17.6796349893608));
#212140=CARTESIAN_POINT('Ctrl Pts',(20.2723747386373,-20.9210649644522,
17.8068107960422));
#212141=CARTESIAN_POINT('Ctrl Pts',(17.9110210446205,-21.3113472211018,
17.9339866027237));
#212142=CARTESIAN_POINT('Ctrl Pts',(16.3046994623321,-19.5370748399901,
18.061162409405));
#212143=CARTESIAN_POINT('Ctrl Pts',(16.9271103439532,-17.2260326070351,
18.1883382160865));
#212144=CARTESIAN_POINT('Ctrl Pts',(19.2072303367862,-16.498458331493,18.3155140227679));
#212145=CARTESIAN_POINT('Ctrl Pts',(21.0531908675876,-18.0218562528634,
18.4426898294494));
#212146=CARTESIAN_POINT('Ctrl Pts',(20.7714377226303,-20.3986033309466,
18.5698656361308));
#212147=CARTESIAN_POINT('Ctrl Pts',(18.6204619247414,-21.4481816393175,
18.6970414428122));
#212148=CARTESIAN_POINT('Ctrl Pts',(16.57365026406,-20.2076682239227,18.8242172494937));
#212149=CARTESIAN_POINT('Ctrl Pts',(16.508825399435,-17.8151571490185,18.9513930561751));
#212150=CARTESIAN_POINT('Ctrl Pts',(18.4854601213826,-16.4656288287323,
19.0785688628566));
#212151=CARTESIAN_POINT('Ctrl Pts',(20.6901147549395,-17.3971917378963,
19.205744669538));
#212152=CARTESIAN_POINT('Ctrl Pts',(21.1001555127428,-19.7551947225373,
19.3329204762194));
#212153=CARTESIAN_POINT('Ctrl Pts',(19.3393954444469,-21.3763164063757,
19.4600962829008));
#212154=CARTESIAN_POINT('Ctrl Pts',(17.0232226373686,-20.7732782473175,
19.5872720895823));
#212155=CARTESIAN_POINT('Ctrl Pts',(16.2765818653196,-18.4993303570677,
19.7144478962637));
#212156=CARTESIAN_POINT('Ctrl Pts',(17.784469731095,-16.6406787308973,19.8416237029452));
#212157=CARTESIAN_POINT('Ctrl Pts',(20.1634926381912,-16.9025209845322,
19.9687995096266));
#212158=CARTESIAN_POINT('Ctrl Pts',(21.2310448625075,-19.0446328907795,
20.095975316308));
#212159=CARTESIAN_POINT('Ctrl Pts',(20.0077132391621,-21.1017601371114,
20.2231511229895));
#212160=CARTESIAN_POINT('Ctrl Pts',(17.6158291027325,-21.1866153706034,
20.3503269296709));
#212161=CARTESIAN_POINT('Ctrl Pts',(16.2497967305417,-19.2213506919733,
20.4775027363524));
#212162=CARTESIAN_POINT('Ctrl Pts',(17.162867889616,-17.0089715551397,20.6046785430338));
#212163=CARTESIAN_POINT('Ctrl Pts',(19.517352896747,-16.5792041101632,20.7318543497152));
#212164=CARTESIAN_POINT('Ctrl Pts',(21.153164764767,-18.3263225093304,20.8590301563966));
#212165=CARTESIAN_POINT('Ctrl Pts',(20.5695343966718,-20.6474748753932,
20.9862059630781));
#212166=CARTESIAN_POINT('Ctrl Pts',(18.3019319358899,-21.4131078753525,
21.1133817697595));
#212167=CARTESIAN_POINT('Ctrl Pts',(16.4306927582234,-19.9208780183909,
21.2405575764409));
#212168=CARTESIAN_POINT('Ctrl Pts',(16.672657339533,-17.5396647158853,21.3677333831224));
#212169=CARTESIAN_POINT('Ctrl Pts',(18.8056557936095,-16.4543701890598,
21.4949091898038));
#212170=CARTESIAN_POINT('Ctrl Pts',(20.8731458592265,-17.6601321897591,
21.6220849964852));
#212171=CARTESIAN_POINT('Ctrl Pts',(20.9776565367662,-20.0518039395808,
21.7492608031667));
#212172=CARTESIAN_POINT('Ctrl Pts',(19.0246114636561,-21.4331200318623,
21.8764366098481));
#212173=CARTESIAN_POINT('Ctrl Pts',(16.8032831871667,-20.5407974041735,
22.0036124165295));
#212174=CARTESIAN_POINT('Ctrl Pts',(16.3565571918356,-18.1855239713029,
22.130788223211));
#212175=CARTESIAN_POINT('Ctrl Pts',(17.5080922582077,-17.0924952631291,
22.2155720943319));
#212176=CARTESIAN_POINT('Ctrl Pts',(18.187758323454,-16.9106265641217,22.2579640298924));
#212177=CARTESIAN_POINT('Ctrl Pts',(20.4651728847368,-17.4941906656173,
-0.084476497129225));
#212178=CARTESIAN_POINT('Ctrl Pts',(20.9507812774351,-18.0708180784204,
-0.0420659055481974));
#212179=CARTESIAN_POINT('Ctrl Pts',(21.2916315045783,-19.7372655677721,
0.0427366215933083));
#212180=CARTESIAN_POINT('Ctrl Pts',(19.454354539323,-21.53119898684,0.169931084295291));
#212181=CARTESIAN_POINT('Ctrl Pts',(16.9568469479949,-20.951919105231,0.297106890976727));
#212182=CARTESIAN_POINT('Ctrl Pts',(16.0896125232803,-18.5411723000033,
0.42428269765816));
#212183=CARTESIAN_POINT('Ctrl Pts',(17.648515078568,-16.5056184191814,0.551458504339596));
#212184=CARTESIAN_POINT('Ctrl Pts',(20.2032439208991,-16.7153568936381,
0.678634311021028));
#212185=CARTESIAN_POINT('Ctrl Pts',(21.41005272189,-18.9766152880434,0.805810117702464));
#212186=CARTESIAN_POINT('Ctrl Pts',(20.1617388362496,-21.2155301029391,
0.932985924383898));
#212187=CARTESIAN_POINT('Ctrl Pts',(17.6035685858491,-21.3776722727239,
1.06016173106533));
#212188=CARTESIAN_POINT('Ctrl Pts',(16.0824961916403,-19.3144751852875,
1.18733753774677));
#212189=CARTESIAN_POINT('Ctrl Pts',(16.9940154259929,-16.918696135723,1.3145133444282));
#212190=CARTESIAN_POINT('Ctrl Pts',(19.5018617560294,-16.3883645566231,
1.44168915110964));
#212191=CARTESIAN_POINT('Ctrl Pts',(21.3052429758379,-18.2100003608074,
1.56886495779107));
#212192=CARTESIAN_POINT('Ctrl Pts',(20.7496681511615,-20.7123794613962,
1.69604076447251));
#212193=CARTESIAN_POINT('Ctrl Pts',(18.344843009889,-21.599717237933,1.82321657115394));
#212194=CARTESIAN_POINT('Ctrl Pts',(16.2970451984157,-20.057940045637,1.95039237783538));
#212195=CARTESIAN_POINT('Ctrl Pts',(16.4850021913768,-17.5015308492868,
2.07756818451681));
#212196=CARTESIAN_POINT('Ctrl Pts',(18.7362750704342,-16.275837412191,2.20474399119824));
#212197=CARTESIAN_POINT('Ctrl Pts',(20.9854607212405,-17.5053568716867,
2.33191979787968));
#212198=CARTESIAN_POINT('Ctrl Pts',(21.1690708977422,-20.0620817041385,
2.45909560456111));
#212199=CARTESIAN_POINT('Ctrl Pts',(19.1186546651756,-21.6003754249779,
2.58627141124255));
#212200=CARTESIAN_POINT('Ctrl Pts',(16.7153416505994,-20.7089490947747,
2.71344721792398));
#212201=CARTESIAN_POINT('Ctrl Pts',(16.1640223800872,-18.2056310058767,
2.84062302460542));
#212202=CARTESIAN_POINT('Ctrl Pts',(17.9704980647556,-16.3870601508454,
2.96779883128685));
#212203=CARTESIAN_POINT('Ctrl Pts',(20.477439386886,-16.9216624058443,3.09497463796828));
#212204=CARTESIAN_POINT('Ctrl Pts',(21.3848832815229,-19.3189733883075,
3.22215044464972));
#212205=CARTESIAN_POINT('Ctrl Pts',(19.8603062977751,-21.3796090630069,
3.34932625133115));
#212206=CARTESIAN_POINT('Ctrl Pts',(17.3024131922505,-21.213064097291,3.47650205801259));
#212207=CARTESIAN_POINT('Ctrl Pts',(16.0579121285487,-18.9721331595253,
3.60367786469402));
#212208=CARTESIAN_POINT('Ctrl Pts',(17.2685555901523,-16.7127312976299,
3.73085367137545));
#212209=CARTESIAN_POINT('Ctrl Pts',(19.8236533420561,-16.5077194854014,
3.85802947805689));
#212210=CARTESIAN_POINT('Ctrl Pts',(21.3790617841357,-18.5451833361938,
3.98520528473832));
#212211=CARTESIAN_POINT('Ctrl Pts',(20.5077902103209,-20.9558762261203,
4.11238109141976));
#212212=CARTESIAN_POINT('Ctrl Pts',(18.009176212373,-21.5281370531764,4.23955689810119));
#212213=CARTESIAN_POINT('Ctrl Pts',(16.1755430519351,-19.7369520270363,
4.36673270478263));
#212214=CARTESIAN_POINT('Ctrl Pts',(16.6891353455996,-17.2256222357103,
4.49390851146406));
#212215=CARTESIAN_POINT('Ctrl Pts',(19.0787640410623,-16.2981368920303,
4.6210843181455));
#212216=CARTESIAN_POINT('Ctrl Pts',(21.15209312732,-17.805406232592,4.74826012482693));
#212217=CARTESIAN_POINT('Ctrl Pts',(21.0069718530473,-20.364604189115,4.87543593150836));
#212218=CARTESIAN_POINT('Ctrl Pts',(18.7765399801474,-21.6278254782292,
5.0026117381898));
#212219=CARTESIAN_POINT('Ctrl Pts',(16.5070803157911,-20.4361429715275,
5.12978754487123));
#212220=CARTESIAN_POINT('Ctrl Pts',(16.2806812434728,-17.8828514047509,
5.25696335155267));
#212221=CARTESIAN_POINT('Ctrl Pts',(18.3050498601331,-16.3104373152697,
5.38413915823409));
#212222=CARTESIAN_POINT('Ctrl Pts',(20.7229536064731,-17.1614930351577,
5.51131496491554));
#212223=CARTESIAN_POINT('Ctrl Pts',(21.3161158672572,-19.6552277638931,
5.63849077159696));
#212224=CARTESIAN_POINT('Ctrl Pts',(19.5403470840179,-21.503794666494,5.76566657827842));
#212225=CARTESIAN_POINT('Ctrl Pts',(17.0248048987365,-21.0112483448259,
5.89284238495983));
#212226=CARTESIAN_POINT('Ctrl Pts',(16.0773431342523,-18.6294694781468,
6.02001819164128));
#212227=CARTESIAN_POINT('Ctrl Pts',(17.5671991533703,-16.5435923467661,
6.1471939983227));
#212228=CARTESIAN_POINT('Ctrl Pts',(20.127522529443,-16.6672797545901,6.27436980500414));
#212229=CARTESIAN_POINT('Ctrl Pts',(21.4093754765144,-18.8870561818465,
6.40154561168558));
#212230=CARTESIAN_POINT('Ctrl Pts',(20.2367374764131,-21.1664145313908,
6.52872141836701));
#212231=CARTESIAN_POINT('Ctrl Pts',(17.6854311121095,-21.4141849904505,
6.65589722504845));
#212232=CARTESIAN_POINT('Ctrl Pts',(16.0961216209204,-19.4030535412072,
6.78307303172988));
#212233=CARTESIAN_POINT('Ctrl Pts',(16.9269018173399,-16.9781084634466,
6.91024883841132));
#212234=CARTESIAN_POINT('Ctrl Pts',(19.4155824351873,-16.3640863569478,
7.03742464509275));
#212235=CARTESIAN_POINT('Ctrl Pts',(21.2789534725274,-18.1243143939139,
7.16460045177418));
#212236=CARTESIAN_POINT('Ctrl Pts',(20.8074876564503,-20.6438926025015,
7.29177625845562));
#212237=CARTESIAN_POINT('Ctrl Pts',(18.4337256107381,-21.6112643589919,
7.41895206513705));
#212238=CARTESIAN_POINT('Ctrl Pts',(16.3354466800433,-20.1389261186678,
7.54612787181849));
#212239=CARTESIAN_POINT('Ctrl Pts',(16.4376915494001,-17.5776568334092,
7.67330367849992));
#212240=CARTESIAN_POINT('Ctrl Pts',(18.646656897206,-16.2772621021406,7.80047948518135));
#212241=CARTESIAN_POINT('Ctrl Pts',(20.9357541207011,-17.4307733792013,
7.92765529186279));
#212242=CARTESIAN_POINT('Ctrl Pts',(21.2048785947256,-19.9799156628723,
8.05483109854422));
#212243=CARTESIAN_POINT('Ctrl Pts',(19.2071253181107,-21.5860091254994,
8.18200690522566));
#212244=CARTESIAN_POINT('Ctrl Pts',(16.7753089275983,-20.7755627005247,
8.3091827119071));
#212245=CARTESIAN_POINT('Ctrl Pts',(16.1404700259359,-18.2921106808846,
8.43635851858852));
#212246=CARTESIAN_POINT('Ctrl Pts',(17.8850339028528,-16.4140661541825,
8.56353432526996));
#212247=CARTESIAN_POINT('Ctrl Pts',(20.4084714811236,-16.8644184090784,
8.69071013195139));
#212248=CARTESIAN_POINT('Ctrl Pts',(21.3956854048846,-19.2299972037186,
8.81788593863284));
#212249=CARTESIAN_POINT('Ctrl Pts',(19.9409681724916,-21.3405308183994,
8.94506174531426));
#212250=CARTESIAN_POINT('Ctrl Pts',(17.3789325547309,-21.2597356561407,
9.0722375519957));
#212251=CARTESIAN_POINT('Ctrl Pts',(16.0600872130337,-19.0617362636017,
9.19941335867713));
#212252=CARTESIAN_POINT('Ctrl Pts',(17.1943908916334,-16.7630606602087,
9.32658916535856));
#212253=CARTESIAN_POINT('Ctrl Pts',(19.7411903682412,-16.4726010401766,
9.45376497204));
#212254=CARTESIAN_POINT('Ctrl Pts',(21.3639551952721,-18.4568360769276,
9.58094077872143));
#212255=CARTESIAN_POINT('Ctrl Pts',(20.5738993640695,-20.8953532797583,
9.70811658540287));
#212256=CARTESIAN_POINT('Ctrl Pts',(18.0958500633667,-21.5509644665186,
9.83529239208431));
#212257=CARTESIAN_POINT('Ctrl Pts',(16.2032637214729,-19.8221870651751,
9.96246819876573));
#212258=CARTESIAN_POINT('Ctrl Pts',(16.6324708399194,-17.2950670414339,
10.0896440054472));
#212259=CARTESIAN_POINT('Ctrl Pts',(18.9897005271298,-16.2880801663194,
10.2168198121286));
#212260=CARTESIAN_POINT('Ctrl Pts',(21.1123408512631,-17.7250743970949,
10.3439956188101));
#212261=CARTESIAN_POINT('Ctrl Pts',(21.0530010608437,-20.2876967169446,
10.4711714254915));
#212262=CARTESIAN_POINT('Ctrl Pts',(18.8661217305387,-21.6249002016856,
10.598347232173));
#212263=CARTESIAN_POINT('Ctrl Pts',(16.5580289128638,-20.5098836502765,
10.7255230388544));
#212264=CARTESIAN_POINT('Ctrl Pts',(16.2462545116391,-17.965605542903,10.8526988455358));
#212265=CARTESIAN_POINT('Ctrl Pts',(18.2168321890867,-16.3262831273715,
10.9798746522173));
#212266=CARTESIAN_POINT('Ctrl Pts',(20.6618792339927,-17.0958929721078,
11.1070504588987));
#212267=CARTESIAN_POINT('Ctrl Pts',(21.3382167393905,-19.5683658119407,
11.2342262655802));
#212268=CARTESIAN_POINT('Ctrl Pts',(19.6253470223175,-21.4753612752947,
11.3614020722615));
#212269=CARTESIAN_POINT('Ctrl Pts',(17.0947217355035,-21.0673293860297,
11.488577878943));
#212270=CARTESIAN_POINT('Ctrl Pts',(16.0680325112813,-18.7186140772312,
11.6157536856244));
#212271=CARTESIAN_POINT('Ctrl Pts',(17.4872029893547,-16.584015867009,11.7429294923059));
#212272=CARTESIAN_POINT('Ctrl Pts',(20.0502323397452,-16.6218961251351,
11.8701052989873));
#212273=CARTESIAN_POINT('Ctrl Pts',(21.4057002130119,-18.797502065893,11.9972811056688));
#212274=CARTESIAN_POINT('Ctrl Pts',(20.3100489652569,-21.1148502719707,
12.1244569123501));
#212275=CARTESIAN_POINT('Ctrl Pts',(17.7684706125095,-21.4479175951428,
12.2516327190316));
#212276=CARTESIAN_POINT('Ctrl Pts',(16.1127055452724,-19.4911354388884,
12.378808525713));
#212277=CARTESIAN_POINT('Ctrl Pts',(16.8618154443651,-17.0397299799731,
12.5059843323945));
#212278=CARTESIAN_POINT('Ctrl Pts',(19.3285384723745,-16.3427135755694,
12.6331601390759));
#212279=CARTESIAN_POINT('Ctrl Pts',(21.2498093531994,-18.0395555150007,
12.7603359457573));
#212280=CARTESIAN_POINT('Ctrl Pts',(20.8629813012026,-20.5735086367272,
12.8875117524388));
#212281=CARTESIAN_POINT('Ctrl Pts',(18.5229450448345,-21.6198282264327,
13.0146875591202));
#212282=CARTESIAN_POINT('Ctrl Pts',(16.3765386102829,-20.2185810024805,
13.1418633658017));
#212283=CARTESIAN_POINT('Ctrl Pts',(16.3929566802409,-17.6553243216352,
13.2690391724831));
#212284=CARTESIAN_POINT('Ctrl Pts',(18.5571366945425,-16.2816870949206,
13.3962149791645));
#212285=CARTESIAN_POINT('Ctrl Pts',(20.8835778142264,-17.3578962203056,
13.5233907858459));
#212286=CARTESIAN_POINT('Ctrl Pts',(21.2379147072037,-19.8965966223211,
13.6505665925274));
#212287=CARTESIAN_POINT('Ctrl Pts',(19.2950652667951,-21.5686882516355,
13.7777423992088));
#212288=CARTESIAN_POINT('Ctrl Pts',(16.8374732677399,-20.8401308200636,
13.9049182058902));
#212289=CARTESIAN_POINT('Ctrl Pts',(16.1198268338089,-18.3793305516987,
14.0320940125717));
#212290=CARTESIAN_POINT('Ctrl Pts',(17.8005220259727,-16.4439189582757,
14.1592698192531));
#212291=CARTESIAN_POINT('Ctrl Pts',(20.3376253211293,-16.809516051569,14.2864456259346));
#212292=CARTESIAN_POINT('Ctrl Pts',(21.4035019163622,-19.140709189997,14.413621432616));
#212293=CARTESIAN_POINT('Ctrl Pts',(20.0202761913079,-21.2987733592159,
14.5407972392974));
#212294=CARTESIAN_POINT('Ctrl Pts',(17.4569718960327,-21.303818628536,14.6679730459788));
#212295=CARTESIAN_POINT('Ctrl Pts',(16.0652616248443,-19.1512162765007,
14.7951488526603));
#212296=CARTESIAN_POINT('Ctrl Pts',(17.1219531722769,-16.8158453555327,
14.9223246593417));
#212297=CARTESIAN_POINT('Ctrl Pts',(19.6575976292351,-16.4402637361534,
15.0495004660232));
#212298=CARTESIAN_POINT('Ctrl Pts',(21.3458985863041,-18.369044242919,15.1766762727046));
#212299=CARTESIAN_POINT('Ctrl Pts',(20.6379447031482,-20.8326504744915,
15.303852079386));
#212300=CARTESIAN_POINT('Ctrl Pts',(18.1832397269893,-21.5708766220509,
15.4310278860674));
#212301=CARTESIAN_POINT('Ctrl Pts',(16.2338231172801,-19.9064460146934,
15.5582036927489));
#212302=CARTESIAN_POINT('Ctrl Pts',(16.578163618988,-17.3663704284554,15.6853794994303));
#212303=CARTESIAN_POINT('Ctrl Pts',(18.9003501939781,-16.2810115588392,
15.8125553061118));
#212304=CARTESIAN_POINT('Ctrl Pts',(21.0699207908507,-17.6461188037487,
15.9397311127932));
#212305=CARTESIAN_POINT('Ctrl Pts',(21.0964290457131,-20.2092909940909,
16.0669069194746));
#212306=CARTESIAN_POINT('Ctrl Pts',(18.955555280017,-21.6189767336345,16.194082726156));
#212307=CARTESIAN_POINT('Ctrl Pts',(16.6114182961767,-20.581876851313,16.3212585328375));
#212308=CARTESIAN_POINT('Ctrl Pts',(16.214618283316,-18.0494661194781,16.4484343395189));
#212309=CARTESIAN_POINT('Ctrl Pts',(18.1291946250482,-16.3450742054518,
16.5756101462004));
#212310=CARTESIAN_POINT('Ctrl Pts',(20.5986423598435,-17.0323749038605,
16.7027859528818));
#212311=CARTESIAN_POINT('Ctrl Pts',(21.3573964622394,-19.4808124826067,
16.8299617595632));
#212312=CARTESIAN_POINT('Ctrl Pts',(19.7093471368785,-21.4440974303654,
16.9571375662447));
#212313=CARTESIAN_POINT('Ctrl Pts',(17.1664773503022,-21.1210376627748,
17.0843133729261));
#212314=CARTESIAN_POINT('Ctrl Pts',(16.0617123033954,-18.8080204652485,
17.2114891796075));
#212315=CARTESIAN_POINT('Ctrl Pts',(17.4086053572432,-16.6270955544791,
17.338664986289));
#212316=CARTESIAN_POINT('Ctrl Pts',(19.9714657325515,-16.579126172631,17.4658407929704));
#212317=CARTESIAN_POINT('Ctrl Pts',(21.3990281040287,-18.708121250235,17.5930165996518));
#212318=CARTESIAN_POINT('Ctrl Pts',(20.3815926003592,-21.0608599439249,
17.7201924063333));
#212319=CARTESIAN_POINT('Ctrl Pts',(17.8525931469884,-21.4788505296758,
17.8473682130147));
#212320=CARTESIAN_POINT('Ctrl Pts',(16.1322297749793,-19.5786125884764,
17.9745440196961));
#212321=CARTESIAN_POINT('Ctrl Pts',(16.7988291003494,-17.1034964893213,
18.1017198263776));
#212322=CARTESIAN_POINT('Ctrl Pts',(19.2408276159067,-16.3242676301314,
18.228895633059));
#212323=CARTESIAN_POINT('Ctrl Pts',(21.2178432511203,-17.955820124861,18.3560714397405));
#212324=CARTESIAN_POINT('Ctrl Pts',(20.9160868681659,-20.5013058250774,
18.4832472464219));
#212325=CARTESIAN_POINT('Ctrl Pts',(18.6124012191849,-21.6253995916595,
18.6104230531033));
#212326=CARTESIAN_POINT('Ctrl Pts',(16.4202749044646,-20.2968151625747,
18.7375988597848));
#212327=CARTESIAN_POINT('Ctrl Pts',(16.3508477586638,-17.7344462908773,
18.8647746664662));
#212328=CARTESIAN_POINT('Ctrl Pts',(18.4678148796782,-16.2891073766096,
18.9919504731476));
#212329=CARTESIAN_POINT('Ctrl Pts',(20.8289903263147,-17.286807168058,19.119126279829));
#212330=CARTESIAN_POINT('Ctrl Pts',(21.2681421801737,-19.8122180263779,
19.2463020865105));
#212331=CARTESIAN_POINT('Ctrl Pts',(19.3823758667575,-21.5484322422587,
19.3734778931919));
#212332=CARTESIAN_POINT('Ctrl Pts',(16.9017649452107,-20.9025810178173,
19.5006536998734));
#212333=CARTESIAN_POINT('Ctrl Pts',(16.1021159518554,-18.4671927970664,
19.6278295065548));
#212334=CARTESIAN_POINT('Ctrl Pts',(17.7170572450437,-16.4765850543542,
19.7550053132362));
#212335=CARTESIAN_POINT('Ctrl Pts',(20.2649803481551,-16.757016959998,19.8821811199177));
#212336=CARTESIAN_POINT('Ctrl Pts',(21.4083240999114,-19.0512094198929,
20.0093569265991));
#212337=CARTESIAN_POINT('Ctrl Pts',(20.0981412947811,-21.2543836816181,
20.1365327332805));
#212338=CARTESIAN_POINT('Ctrl Pts',(17.5364438714413,-21.345263264656,20.2637085399619));
#212339=CARTESIAN_POINT('Ctrl Pts',(16.0734291899427,-19.2404734101847,
20.3908843466434));
#212340=CARTESIAN_POINT('Ctrl Pts',(17.0513243981187,-16.8710250544057,
20.5180601533248));
#212341=CARTESIAN_POINT('Ctrl Pts',(19.5729675179493,-16.4107460050722,
20.6452359600063));
#212342=CARTESIAN_POINT('Ctrl Pts',(21.3249148566822,-18.2819021506609,
20.7724117666877));
#212343=CARTESIAN_POINT('Ctrl Pts',(20.6998492912724,-20.7678461580482,
20.8995875733692));
#212344=CARTESIAN_POINT('Ctrl Pts',(18.2712569976611,-21.5878357442275,
21.0267633800505));
#212345=CARTESIAN_POINT('Ctrl Pts',(16.2671680424845,-19.989664109829,21.153939186732));
#212346=CARTESIAN_POINT('Ctrl Pts',(16.5263110482178,-17.4393951028376,
21.2811149934134));
#212347=CARTESIAN_POINT('Ctrl Pts',(18.8107430407941,-16.2770494228818,
21.4082908000949));
#212348=CARTESIAN_POINT('Ctrl Pts',(21.0250158365398,-17.568415239189,21.5354666067763));
#212349=CARTESIAN_POINT('Ctrl Pts',(21.1369463139771,-20.1298851974028,
21.6626424134577));
#212350=CARTESIAN_POINT('Ctrl Pts',(19.0452436034431,-21.6092686761098,
21.7898182201392));
#212351=CARTESIAN_POINT('Ctrl Pts',(16.6662107583285,-20.6535950540795,
21.9169940268206));
#212352=CARTESIAN_POINT('Ctrl Pts',(16.1877691759169,-18.1311075337387,
22.044169833502));
#212353=CARTESIAN_POINT('Ctrl Pts',(17.4210581833076,-16.960478579468,22.128953704623));
#212354=CARTESIAN_POINT('Ctrl Pts',(18.1489775593156,-16.7656980002009,
22.1713456401835));
#212355=CARTESIAN_POINT('Ctrl Pts',(20.5799312301559,-17.397553415447,-0.171094886838164));
#212356=CARTESIAN_POINT('Ctrl Pts',(21.0977302932136,-18.0124050913494,
-0.128684295257136));
#212357=CARTESIAN_POINT('Ctrl Pts',(21.4611752643293,-19.7893203209783,
-0.0438817681156302));
#212358=CARTESIAN_POINT('Ctrl Pts',(19.5021063818899,-21.7021724412225,
0.0833126945863534));
#212359=CARTESIAN_POINT('Ctrl Pts',(16.8390406066394,-21.0844924660501,
0.210488501267787));
#212360=CARTESIAN_POINT('Ctrl Pts',(15.9143177655174,-18.5139387940262,
0.337664307949223));
#212361=CARTESIAN_POINT('Ctrl Pts',(17.5765589760555,-16.343449345859,0.464840114630657));
#212362=CARTESIAN_POINT('Ctrl Pts',(20.3006391625102,-16.567091249899,0.592015921312092));
#212363=CARTESIAN_POINT('Ctrl Pts',(21.5874465485414,-18.9782470197745,
0.719191727993526));
#212364=CARTESIAN_POINT('Ctrl Pts',(20.2563827322944,-21.3655780685178,
0.846367534674961));
#212365=CARTESIAN_POINT('Ctrl Pts',(17.5286330090264,-21.5384685392327,
0.973543341356394));
#212366=CARTESIAN_POINT('Ctrl Pts',(15.906729696796,-19.3385034339308,1.10071914803782));
#212367=CARTESIAN_POINT('Ctrl Pts',(16.8786729593171,-16.7839097205383,
1.22789495471926));
#212368=CARTESIAN_POINT('Ctrl Pts',(19.5527628216649,-16.2184227996018,
1.35507076140069));
#212369=CARTESIAN_POINT('Ctrl Pts',(21.4756890313297,-18.1608136783876,
1.48224656808212));
#212370=CARTESIAN_POINT('Ctrl Pts',(20.8832855061817,-20.8290738921377,
1.60942237476356));
#212371=CARTESIAN_POINT('Ctrl Pts',(18.3190460414365,-21.7752327234411,
1.73659818144499));
#212372=CARTESIAN_POINT('Ctrl Pts',(16.1355010202711,-20.1312521052755,
1.86377398812643));
#212373=CARTESIAN_POINT('Ctrl Pts',(16.3359175623115,-17.4053801752063,
1.99094979480786));
#212374=CARTESIAN_POINT('Ctrl Pts',(18.7364258834009,-16.0984363025981,
2.1181256014893));
#212375=CARTESIAN_POINT('Ctrl Pts',(21.134708615211,-17.4094598221888,2.24530140817073));
#212376=CARTESIAN_POINT('Ctrl Pts',(21.3304901931038,-20.135668311675,2.37247721485217));
#212377=CARTESIAN_POINT('Ctrl Pts',(19.1441531773822,-21.7759345412849,
2.49965302153361));
#212378=CARTESIAN_POINT('Ctrl Pts',(16.5815260772467,-20.8254161287028,
2.62682882821504));
#212379=CARTESIAN_POINT('Ctrl Pts',(15.993660204232,-18.1561546817078,2.75400463489647));
#212380=CARTESIAN_POINT('Ctrl Pts',(17.9198860088567,-16.2170319255978,
2.8811804415779));
#212381=CARTESIAN_POINT('Ctrl Pts',(20.5930108709022,-16.7870726228123,
3.00835624825935));
#212382=CARTESIAN_POINT('Ctrl Pts',(21.5606086420394,-19.3432998199575,
3.13553205494078));
#212383=CARTESIAN_POINT('Ctrl Pts',(19.9349684232667,-21.5405337181072,
3.26270786162222));
#212384=CARTESIAN_POINT('Ctrl Pts',(17.2075142166313,-21.3629485929295,
3.38988366830364));
#212385=CARTESIAN_POINT('Ctrl Pts',(15.8805159718554,-18.9734677738182,
3.51705947498509));
#212386=CARTESIAN_POINT('Ctrl Pts',(17.1714122157033,-16.5642916048074,
3.64423528166652));
#212387=CARTESIAN_POINT('Ctrl Pts',(19.8958857665108,-16.3456896904175,
3.77141108834796));
#212388=CARTESIAN_POINT('Ctrl Pts',(21.5544012413067,-18.5182157192451,
3.89858689502939));
#212389=CARTESIAN_POINT('Ctrl Pts',(20.6253736310478,-21.0887119019572,
4.02576270171082));
#212390=CARTESIAN_POINT('Ctrl Pts',(17.9611281061891,-21.6989075339308,
4.15293850839226));
#212391=CARTESIAN_POINT('Ctrl Pts',(16.0059445740623,-19.7889859958273,
4.28011431507369));
#212392=CARTESIAN_POINT('Ctrl Pts',(16.5535825730174,-17.1111817557645,
4.40729012175513));
#212393=CARTESIAN_POINT('Ctrl Pts',(19.101618229261,-16.1222140007207,4.53446592843656));
#212394=CARTESIAN_POINT('Ctrl Pts',(21.3123869771181,-17.7293992636892,
4.661641735118));
#212395=CARTESIAN_POINT('Ctrl Pts',(21.1576457062134,-20.4582448190628,
4.78881754179943));
#212396=CARTESIAN_POINT('Ctrl Pts',(18.7793599282756,-21.8052042410433,
4.91599334848086));
#212397=CARTESIAN_POINT('Ctrl Pts',(16.3594592314995,-20.5345258616938,
5.0431691551623));
#212398=CARTESIAN_POINT('Ctrl Pts',(16.1180523092011,-17.8119782268727,
5.17034496184372));
#212399=CARTESIAN_POINT('Ctrl Pts',(18.2766150291857,-16.1353298111647,
5.29752076852517));
#212400=CARTESIAN_POINT('Ctrl Pts',(20.8548000713794,-17.0428014714449,
5.4246965752066));
#212401=CARTESIAN_POINT('Ctrl Pts',(21.4872826797803,-19.7018442834496,
5.55187238188803));
#212402=CARTESIAN_POINT('Ctrl Pts',(19.5937993174784,-21.6729515059744,
5.67904818856948));
#212403=CARTESIAN_POINT('Ctrl Pts',(16.9115034465541,-21.1477546030643,
5.8062239952509));
#212404=CARTESIAN_POINT('Ctrl Pts',(15.901235046523,-18.6080891357435,5.93339980193234));
#212405=CARTESIAN_POINT('Ctrl Pts',(17.4898526700851,-16.3839405408623,
6.06057560861377));
#212406=CARTESIAN_POINT('Ctrl Pts',(20.2198982483519,-16.515827107994,6.1877514152952));
#212407=CARTESIAN_POINT('Ctrl Pts',(21.5867244090021,-18.8827510975986,
6.31492722197664));
#212408=CARTESIAN_POINT('Ctrl Pts',(20.3363529844384,-21.3132066570849,
6.44210302865808));
#212409=CARTESIAN_POINT('Ctrl Pts',(17.6159221498948,-21.577401661709,6.56927883533951));
#212410=CARTESIAN_POINT('Ctrl Pts',(15.921258347085,-19.4329535925197,6.69645464202095));
#212411=CARTESIAN_POINT('Ctrl Pts',(16.8071104323889,-16.8472604535401,
6.82363044870238));
#212412=CARTESIAN_POINT('Ctrl Pts',(19.4607640997214,-16.1925352135684,
6.95080625538382));
#212413=CARTESIAN_POINT('Ctrl Pts',(21.4476568136269,-18.0694476434471,
7.07798206206525));
#212414=CARTESIAN_POINT('Ctrl Pts',(20.9449378295665,-20.7560470830862,
7.20515786874668));
#212415=CARTESIAN_POINT('Ctrl Pts',(18.4138206131569,-21.7875452957837,
7.33233367542812));
#212416=CARTESIAN_POINT('Ctrl Pts',(16.1764481116018,-20.2176066933892,
7.45950948210955));
#212417=CARTESIAN_POINT('Ctrl Pts',(16.2854707280793,-17.4865525022204,
7.586685288791));
#212418=CARTESIAN_POINT('Ctrl Pts',(18.6408669786781,-16.0999554343349,
7.7138610954724));
#212419=CARTESIAN_POINT('Ctrl Pts',(21.0817069958525,-17.3299322375973,
7.84103690215387));
#212420=CARTESIAN_POINT('Ctrl Pts',(21.3686715594619,-20.0480555359847,
7.96821270883528));
#212421=CARTESIAN_POINT('Ctrl Pts',(19.2384884934243,-21.7606159089848,
8.09538851551673));
#212422=CARTESIAN_POINT('Ctrl Pts',(16.6454685467572,-20.8964455078546,
8.22256432219815));
#212423=CARTESIAN_POINT('Ctrl Pts',(15.9685465795588,-18.2483670391668,
8.3497401288796));
#212424=CARTESIAN_POINT('Ctrl Pts',(17.8287564822182,-16.2458281396566,
8.47691593556102));
#212425=CARTESIAN_POINT('Ctrl Pts',(20.5194711266932,-16.726033958043,8.60409174224246));
#212426=CARTESIAN_POINT('Ctrl Pts',(21.5721268312631,-19.248425460891,8.7312675489239));
#212427=CARTESIAN_POINT('Ctrl Pts',(20.0209773221669,-21.4988650016106,
8.85844335560533));
#212428=CARTESIAN_POINT('Ctrl Pts',(17.2891059988037,-21.4127139796221,
8.98561916228676));
#212429=CARTESIAN_POINT('Ctrl Pts',(15.8828352413023,-19.0690106104647,
9.1127949689682));
#212430=CARTESIAN_POINT('Ctrl Pts',(17.0923311866634,-16.6179572687033,
9.23997077564963));
#212431=CARTESIAN_POINT('Ctrl Pts',(19.8079563748028,-16.308243265877,9.36714658233107));
#212432=CARTESIAN_POINT('Ctrl Pts',(21.5382932463107,-18.4240119765596,
9.4943223890125));
#212433=CARTESIAN_POINT('Ctrl Pts',(20.6958651183971,-21.0241769281162,
9.62149819569394));
#212434=CARTESIAN_POINT('Ctrl Pts',(18.0535475114361,-21.7232481619313,
9.74867400237537));
#212435=CARTESIAN_POINT('Ctrl Pts',(16.0355028290879,-19.8798712102337,
9.8758498090568));
#212436=CARTESIAN_POINT('Ctrl Pts',(16.4931618134281,-17.1852300133289,
10.0030256157383));
#212437=CARTESIAN_POINT('Ctrl Pts',(19.0066507518444,-16.1114906210823,
10.1302014224197));
#212438=CARTESIAN_POINT('Ctrl Pts',(21.2699995480578,-17.6437422820976,
10.2573772291012));
#212439=CARTESIAN_POINT('Ctrl Pts',(21.2067261608115,-20.3762391996566,
10.3845530357826));
#212440=CARTESIAN_POINT('Ctrl Pts',(18.874879995715,-21.802085049785,10.511728842464));
#212441=CARTESIAN_POINT('Ctrl Pts',(16.4137851785486,-20.613154762964,10.6389046491454));
#212442=CARTESIAN_POINT('Ctrl Pts',(16.0813434512909,-17.9002180840159,
10.7660804558269));
#212443=CARTESIAN_POINT('Ctrl Pts',(18.1825494650401,-16.1522260320353,
10.8932562625083));
#212444=CARTESIAN_POINT('Ctrl Pts',(20.7896771177347,-16.9728528220917,
11.0204320691897));
#212445=CARTESIAN_POINT('Ctrl Pts',(21.5108486046191,-19.6092243081515,
11.1476078758712));
#212446=CARTESIAN_POINT('Ctrl Pts',(19.6844338474274,-21.6426332834231,
11.2747836825526));
#212447=CARTESIAN_POINT('Ctrl Pts',(16.9860550257985,-21.2075532206898,
11.4019594892341));
#212448=CARTESIAN_POINT('Ctrl Pts',(15.8913072282989,-18.7031430733949,
11.5291352959155));
#212449=CARTESIAN_POINT('Ctrl Pts',(17.4045536114233,-16.4270437104573,
11.6563111025969));
#212450=CARTESIAN_POINT('Ctrl Pts',(20.1374845413179,-16.4674350267135,
11.7834869092783));
#212451=CARTESIAN_POINT('Ctrl Pts',(21.5828055146281,-18.7872604964663,
11.9106627159598));
#212452=CARTESIAN_POINT('Ctrl Pts',(20.4145242450785,-21.2582242358244,
12.0378385226412));
#212453=CARTESIAN_POINT('Ctrl Pts',(17.7044662857673,-21.613370379233,12.1650143293227));
#212454=CARTESIAN_POINT('Ctrl Pts',(15.9389416091958,-19.5268743829703,
12.2921901360041));
#212455=CARTESIAN_POINT('Ctrl Pts',(16.7377095252982,-16.9129668210605,
12.4193659426856));
#212456=CARTESIAN_POINT('Ctrl Pts',(19.3679500481791,-16.1697456441558,
12.5465417493669));
#212457=CARTESIAN_POINT('Ctrl Pts',(21.416580749233,-17.9790701525573,12.6737175560484));
#212458=CARTESIAN_POINT('Ctrl Pts',(21.0041101126047,-20.6809974091509,
12.8008933627298));
#212459=CARTESIAN_POINT('Ctrl Pts',(18.5089543465855,-21.7966768565304,
12.9280691694113));
#212460=CARTESIAN_POINT('Ctrl Pts',(16.2202639996657,-20.3025418486013,
13.0552449760927));
#212461=CARTESIAN_POINT('Ctrl Pts',(16.2377704130005,-17.5693685186612,
13.1824207827741));
#212462=CARTESIAN_POINT('Ctrl Pts',(18.545412538926,-16.1046737570615,13.3095965894556));
#212463=CARTESIAN_POINT('Ctrl Pts',(21.0260719553289,-17.2522240983603,
13.436772396137));
#212464=CARTESIAN_POINT('Ctrl Pts',(21.4038976147472,-19.9592133294229,
13.5639482028184));
#212465=CARTESIAN_POINT('Ctrl Pts',(19.3322579251698,-21.7421468454496,
13.6911240094999));
#212466=CARTESIAN_POINT('Ctrl Pts',(16.7117537213236,-20.96529380682,13.8182998161813));
#212467=CARTESIAN_POINT('Ctrl Pts',(15.9465349634034,-18.3413686595396,
13.9454756228628));
#212468=CARTESIAN_POINT('Ctrl Pts',(17.7386423669686,-16.2776598670762,
14.0726514295442));
#212469=CARTESIAN_POINT('Ctrl Pts',(20.443928619978,-16.6674921583018,14.1998272362256));
#212470=CARTESIAN_POINT('Ctrl Pts',(21.5804614942969,-19.1532186017375,
14.327003042907));
#212471=CARTESIAN_POINT('Ctrl Pts',(20.1055426189236,-21.454339467114,14.4541788495885));
#212472=CARTESIAN_POINT('Ctrl Pts',(17.3723185182233,-21.4597191841168,
14.5813546562699));
#212473=CARTESIAN_POINT('Ctrl Pts',(15.8883526615688,-19.1644221962985,
14.7085304629514));
#212474=CARTESIAN_POINT('Ctrl Pts',(17.015091617132,-16.6742410277849,14.8357062696328));
#212475=CARTESIAN_POINT('Ctrl Pts',(19.7188223264901,-16.2737623426128,
14.9628820763142));
#212476=CARTESIAN_POINT('Ctrl Pts',(21.5190396762608,-18.3304004779172,
15.0900578829957));
#212477=CARTESIAN_POINT('Ctrl Pts',(20.7641559821193,-20.9573175939151,
15.2172336896771));
#212478=CARTESIAN_POINT('Ctrl Pts',(18.1467301800744,-21.7444802815428,
15.3444094963585));
#212479=CARTESIAN_POINT('Ctrl Pts',(16.0680879877353,-19.9697156317281,
15.4715853030399));
#212480=CARTESIAN_POINT('Ctrl Pts',(16.4352546014886,-17.2612600563589,
15.5987611097214));
#212481=CARTESIAN_POINT('Ctrl Pts',(18.9113774421457,-16.1039534401246,
15.7259369164028));
#212482=CARTESIAN_POINT('Ctrl Pts',(21.2247674889198,-17.5595527728704,
15.8531127230842));
#212483=CARTESIAN_POINT('Ctrl Pts',(21.2530329590753,-20.2926360114859,
15.9802885297657));
#212484=CARTESIAN_POINT('Ctrl Pts',(18.9702420380974,-21.7957689188181,
16.1074643364471));
#212485=CARTESIAN_POINT('Ctrl Pts',(16.4707137099997,-20.6899203473398,
16.2346401431286));
#212486=CARTESIAN_POINT('Ctrl Pts',(16.0476100775874,-17.9896377246791,
16.36181594981));
#212487=CARTESIAN_POINT('Ctrl Pts',(18.0891024628257,-16.1722627586861,
16.4889917564914));
#212488=CARTESIAN_POINT('Ctrl Pts',(20.722248311566,-16.9051241816477,16.6161675631729));
#212489=CARTESIAN_POINT('Ctrl Pts',(21.5312997390521,-19.5158671245064,
16.7433433698543));
#212490=CARTESIAN_POINT('Ctrl Pts',(19.7740022759604,-21.6092969781711,
16.8705191765357));
#212491=CARTESIAN_POINT('Ctrl Pts',(17.062567274496,-21.2648217848151,16.9976949832172));
#212492=CARTESIAN_POINT('Ctrl Pts',(15.8845680578669,-18.7984761538005,
17.1248707898986));
#212493=CARTESIAN_POINT('Ctrl Pts',(17.3207457924527,-16.4729791229096,
17.25204659658));
#212494=CARTESIAN_POINT('Ctrl Pts',(20.0534965460147,-16.4218298813604,
17.3792224032615));
#212495=CARTESIAN_POINT('Ctrl Pts',(21.5756911157996,-18.6919546835953,
17.5063982099429));
#212496=CARTESIAN_POINT('Ctrl Pts',(20.4908104620813,-21.2006549233978,
17.6335740166243));
#212497=CARTESIAN_POINT('Ctrl Pts',(17.7941652493564,-21.6463538382498,
17.7607498233058));
#212498=CARTESIAN_POINT('Ctrl Pts',(15.9597600876265,-19.6201503369626,
17.8879256299872));
#212499=CARTESIAN_POINT('Ctrl Pts',(16.6705478567457,-16.9809603716076,
18.0151014366687));
#212500=CARTESIAN_POINT('Ctrl Pts',(19.2744248950271,-16.1500769287699,
18.1422772433501));
#212501=CARTESIAN_POINT('Ctrl Pts',(21.382495634653,-17.8897839968585,18.2694530500315));
#212502=CARTESIAN_POINT('Ctrl Pts',(21.0607360137015,-20.6040083192082,
18.3966288567129));
#212503=CARTESIAN_POINT('Ctrl Pts',(18.6043405136283,-21.8026175440015,
18.5238046633944));
#212504=CARTESIAN_POINT('Ctrl Pts',(16.2668995448691,-20.3859621012267,
18.6509804700758));
#212505=CARTESIAN_POINT('Ctrl Pts',(16.1928701178928,-17.6537354327361,
18.7781562767572));
#212506=CARTESIAN_POINT('Ctrl Pts',(18.4501696379737,-16.1125859244869,
18.9053320834387));
#212507=CARTESIAN_POINT('Ctrl Pts',(20.9678658976898,-17.1764225982197,
19.0325078901201));
#212508=CARTESIAN_POINT('Ctrl Pts',(21.4361288476046,-19.8692413302184,
19.1596836968015));
#212509=CARTESIAN_POINT('Ctrl Pts',(19.4253562890682,-21.7205480781417,
19.286859503483));
#212510=CARTESIAN_POINT('Ctrl Pts',(16.7803072530527,-21.0318837883171,
19.4140353101644));
#212511=CARTESIAN_POINT('Ctrl Pts',(15.9276500383912,-18.435055237065,19.5412111168458));
#212512=CARTESIAN_POINT('Ctrl Pts',(17.6496447589923,-16.3124913778111,
19.6683869235273));
#212513=CARTESIAN_POINT('Ctrl Pts',(20.366468058119,-16.6115129354638,19.7955627302087));
#212514=CARTESIAN_POINT('Ctrl Pts',(21.5856033373152,-19.0577859490064,
19.9227385368901));
#212515=CARTESIAN_POINT('Ctrl Pts',(20.1885693504001,-21.4070072261248,
20.0499143435716));
#212516=CARTESIAN_POINT('Ctrl Pts',(17.45705864015,-21.5039111587085,20.177090150253));
#212517=CARTESIAN_POINT('Ctrl Pts',(15.8970616493438,-19.2595961283962,
20.3042659569345));
#212518=CARTESIAN_POINT('Ctrl Pts',(16.9397809066213,-16.7330785536716,
20.4314417636159));
#212519=CARTESIAN_POINT('Ctrl Pts',(19.6285821391517,-16.2422878999811,
20.5586175702973));
#212520=CARTESIAN_POINT('Ctrl Pts',(21.4966649485975,-18.2374817919912,
20.6857933769788));
#212521=CARTESIAN_POINT('Ctrl Pts',(20.8301641858729,-20.8882174407032,
20.8129691836602));
#212522=CARTESIAN_POINT('Ctrl Pts',(18.2405820594323,-21.7625636131024,
20.9401449903416));
#212523=CARTESIAN_POINT('Ctrl Pts',(16.1036433267455,-20.0584502012673,
21.0673207970231));
#212524=CARTESIAN_POINT('Ctrl Pts',(16.3799647569026,-17.3391254897899,
21.1944966037045));
#212525=CARTESIAN_POINT('Ctrl Pts',(18.8158302879787,-16.0997286567039,
21.3216724103859));
#212526=CARTESIAN_POINT('Ctrl Pts',(21.1768858138531,-17.4766982886188,
21.4488482170674));
#212527=CARTESIAN_POINT('Ctrl Pts',(21.2962360911878,-20.207966455225,21.5760240237488));
#212528=CARTESIAN_POINT('Ctrl Pts',(19.0658757432302,-21.7854173203574,
21.7031998304302));
#212529=CARTESIAN_POINT('Ctrl Pts',(16.5291383294904,-20.7663927039858,
21.8303756371117));
#212530=CARTESIAN_POINT('Ctrl Pts',(16.0189811599981,-18.0766910961744,
21.9575514437931));
#212531=CARTESIAN_POINT('Ctrl Pts',(17.3340241084075,-16.828461895807,22.0423353149141));
#212532=CARTESIAN_POINT('Ctrl Pts',(18.110196795177,-16.6207694362802,22.0847272504745));
#212533=CARTESIAN_POINT('Ctrl Pts',(20.694689575575,-17.3009161652768,-0.257713276547101));
#212534=CARTESIAN_POINT('Ctrl Pts',(21.2446793089921,-17.9539921042784,
-0.215302684966074));
#212535=CARTESIAN_POINT('Ctrl Pts',(21.6307190240804,-19.8413750741844,
-0.130500157824568));
#212536=CARTESIAN_POINT('Ctrl Pts',(19.5498582244566,-21.8731458956047,
-0.00330569512258456));
#212537=CARTESIAN_POINT('Ctrl Pts',(16.721234265284,-21.2170658268692,0.123870111558849));
#212538=CARTESIAN_POINT('Ctrl Pts',(15.7390230077546,-18.486705288049,0.251045918240284));
#212539=CARTESIAN_POINT('Ctrl Pts',(17.504602873543,-16.1812802725366,0.378221724921718));
#212540=CARTESIAN_POINT('Ctrl Pts',(20.3980344041213,-16.4188256061599,
0.505397531603153));
#212541=CARTESIAN_POINT('Ctrl Pts',(21.7648403751927,-18.9798787515055,
0.632573338284587));
#212542=CARTESIAN_POINT('Ctrl Pts',(20.3510266283393,-21.5156260340964,
0.759749144966022));
#212543=CARTESIAN_POINT('Ctrl Pts',(17.4536974322035,-21.6992648057414,
0.886924951647455));
#212544=CARTESIAN_POINT('Ctrl Pts',(15.7309632019515,-19.3625316825742,
1.01410075832889));
#212545=CARTESIAN_POINT('Ctrl Pts',(16.7633304926413,-16.6491233053535,
1.14127656501032));
#212546=CARTESIAN_POINT('Ctrl Pts',(19.6036638873005,-16.0484810425805,
1.26845237169176));
#212547=CARTESIAN_POINT('Ctrl Pts',(21.6461350868215,-18.1116269959678,
1.39562817837319));
#212548=CARTESIAN_POINT('Ctrl Pts',(21.0169028612021,-20.9457683228794,
1.52280398505463));
#212549=CARTESIAN_POINT('Ctrl Pts',(18.293249072984,-21.9507482089492,1.64997979173606));
#212550=CARTESIAN_POINT('Ctrl Pts',(15.9739568421265,-20.2045641649137,
1.7771555984175));
#212551=CARTESIAN_POINT('Ctrl Pts',(16.1868329332462,-17.3092295011259,
1.90433140509893));
#212552=CARTESIAN_POINT('Ctrl Pts',(18.7365766963677,-15.9210351930051,
2.03150721178036));
#212553=CARTESIAN_POINT('Ctrl Pts',(21.2839565091815,-17.3135627726908,
2.1586830184618));
#212554=CARTESIAN_POINT('Ctrl Pts',(21.4919094884653,-20.2092549192115,
2.28585882514323));
#212555=CARTESIAN_POINT('Ctrl Pts',(19.1696516895889,-21.951493657592,2.41303463182467));
#212556=CARTESIAN_POINT('Ctrl Pts',(16.4477105038941,-20.9418831626308,
2.5402104385061));
#212557=CARTESIAN_POINT('Ctrl Pts',(15.8232980283766,-18.1066783575389,
2.66738624518754));
#212558=CARTESIAN_POINT('Ctrl Pts',(17.8692739529578,-16.0470037003502,
2.79456205186897));
#212559=CARTESIAN_POINT('Ctrl Pts',(20.7085823549184,-16.6524828397803,
2.9217378585504));
#212560=CARTESIAN_POINT('Ctrl Pts',(21.7363340025561,-19.3676262516076,
3.04891366523184));
#212561=CARTESIAN_POINT('Ctrl Pts',(20.0096305487582,-21.7014583732074,
3.17608947191327));
#212562=CARTESIAN_POINT('Ctrl Pts',(17.1126152410121,-21.5128330885679,
3.30326527859471));
#212563=CARTESIAN_POINT('Ctrl Pts',(15.703119815162,-18.9748023881108,3.43044108527614));
#212564=CARTESIAN_POINT('Ctrl Pts',(17.0742688412544,-16.4158519119851,
3.55761689195758));
#212565=CARTESIAN_POINT('Ctrl Pts',(19.9681181909656,-16.1836598954335,
3.68479269863901));
#212566=CARTESIAN_POINT('Ctrl Pts',(21.7297406984776,-18.4912481022967,
3.81196850532045));
#212567=CARTESIAN_POINT('Ctrl Pts',(20.7429570517748,-21.221547577794,3.93914431200188));
#212568=CARTESIAN_POINT('Ctrl Pts',(17.9130800000052,-21.8696780146852,
4.06632011868332));
#212569=CARTESIAN_POINT('Ctrl Pts',(15.8363460961894,-19.8410199646181,
4.19349592536474));
#212570=CARTESIAN_POINT('Ctrl Pts',(16.4180298004353,-16.9967412758189,
4.32067173204619));
#212571=CARTESIAN_POINT('Ctrl Pts',(19.1244724174598,-15.9462911094113,
4.44784753872761));
#212572=CARTESIAN_POINT('Ctrl Pts',(21.4726808269163,-17.6533922947864,
4.57502334540905));
#212573=CARTESIAN_POINT('Ctrl Pts',(21.3083195593796,-20.5518854490104,
4.70219915209049));
#212574=CARTESIAN_POINT('Ctrl Pts',(18.7821798764038,-21.9825830038574,
4.82937495877192));
#212575=CARTESIAN_POINT('Ctrl Pts',(16.2118381472079,-20.6329087518601,
4.95655076545335));
#212576=CARTESIAN_POINT('Ctrl Pts',(15.9554233749293,-17.7411050489944,
5.08372657213479));
#212577=CARTESIAN_POINT('Ctrl Pts',(18.2481801982382,-15.9602223070596,
5.21090237881622));
#212578=CARTESIAN_POINT('Ctrl Pts',(20.9866465362858,-16.9241099077319,
5.33807818549766));
#212579=CARTESIAN_POINT('Ctrl Pts',(21.6584494923035,-19.7484608030062,
5.46525399217908));
#212580=CARTESIAN_POINT('Ctrl Pts',(19.6472515509388,-21.8421083454548,
5.59242979886053));
#212581=CARTESIAN_POINT('Ctrl Pts',(16.7982019943716,-21.2842608613029,
5.71960560554195));
#212582=CARTESIAN_POINT('Ctrl Pts',(15.7251269587939,-18.5867087933401,
5.8467814122234));
#212583=CARTESIAN_POINT('Ctrl Pts',(17.4125061868001,-16.2242887349586,
5.97395721890483));
#212584=CARTESIAN_POINT('Ctrl Pts',(20.3122739672608,-16.3643744613978,
6.10113302558626));
#212585=CARTESIAN_POINT('Ctrl Pts',(21.7640733414898,-18.8784460133507,
6.2283088322677));
#212586=CARTESIAN_POINT('Ctrl Pts',(20.4359684924635,-21.459998782779,6.35548463894913));
#212587=CARTESIAN_POINT('Ctrl Pts',(17.54641318768,-21.7406183329676,6.48266044563057));
#212588=CARTESIAN_POINT('Ctrl Pts',(15.7463950732497,-19.4628536438322,
6.609836252312));
#212589=CARTESIAN_POINT('Ctrl Pts',(16.687319047438,-16.7164124436336,6.73701205899344));
#212590=CARTESIAN_POINT('Ctrl Pts',(19.5059457642557,-16.0209840701888,
6.86418786567487));
#212591=CARTESIAN_POINT('Ctrl Pts',(21.6163601547263,-18.0145808929804,
6.99136367235631));
#212592=CARTESIAN_POINT('Ctrl Pts',(21.0823880026828,-20.8682015636709,
7.11853947903774));
#212593=CARTESIAN_POINT('Ctrl Pts',(18.3939156155757,-21.9638262325756,
7.24571528571917));
#212594=CARTESIAN_POINT('Ctrl Pts',(16.0174495431603,-20.2962872681105,
7.37289109240061));
#212595=CARTESIAN_POINT('Ctrl Pts',(16.1332499067586,-17.3954481710317,
7.50006689908204));
#212596=CARTESIAN_POINT('Ctrl Pts',(18.6350770601501,-15.9226487665292,
7.62724270576348));
#212597=CARTESIAN_POINT('Ctrl Pts',(21.2276598710039,-17.2290910959936,
7.75441851244491));
#212598=CARTESIAN_POINT('Ctrl Pts',(21.5324645241983,-20.1161954090971,
7.88159431912634));
#212599=CARTESIAN_POINT('Ctrl Pts',(19.2698516687381,-21.9352226924704,
8.00877012580778));
#212600=CARTESIAN_POINT('Ctrl Pts',(16.515628165916,-21.0173283151844,8.13594593248921));
#212601=CARTESIAN_POINT('Ctrl Pts',(15.7966231331818,-18.2046233974491,
8.26312173917066));
#212602=CARTESIAN_POINT('Ctrl Pts',(17.7724790615836,-16.0775901251306,
8.39029754585207));
#212603=CARTESIAN_POINT('Ctrl Pts',(20.6304707722626,-16.5876495070077,
8.51747335253352));
#212604=CARTESIAN_POINT('Ctrl Pts',(21.7485682576417,-19.2668537180634,
8.64464915921496));
#212605=CARTESIAN_POINT('Ctrl Pts',(20.1009864718422,-21.6571991848217,
8.77182496589638));
#212606=CARTESIAN_POINT('Ctrl Pts',(17.1992794428765,-21.5656923031035,
8.89900077257782));
#212607=CARTESIAN_POINT('Ctrl Pts',(15.7055832695711,-19.0762849573277,
9.02617657925926));
#212608=CARTESIAN_POINT('Ctrl Pts',(16.9902714816934,-16.4728538771981,
9.15335238594069));
#212609=CARTESIAN_POINT('Ctrl Pts',(19.8747223813643,-16.1438854915773,
9.28052819262213));
#212610=CARTESIAN_POINT('Ctrl Pts',(21.7126312973492,-18.3911878761916,
9.40770399930354));
#212611=CARTESIAN_POINT('Ctrl Pts',(20.8178308727247,-21.1530005764741,
9.53487980598502));
#212612=CARTESIAN_POINT('Ctrl Pts',(18.0112449595055,-21.8955318573441,
9.66205561266641));
#212613=CARTESIAN_POINT('Ctrl Pts',(15.8677419367031,-19.9375553552922,
9.78923141934788));
#212614=CARTESIAN_POINT('Ctrl Pts',(16.3538527869367,-17.0753929852239,
9.91640722602929));
#212615=CARTESIAN_POINT('Ctrl Pts',(19.0236009765592,-15.9349010758452,
10.0435830327108));
#212616=CARTESIAN_POINT('Ctrl Pts',(21.4276582448523,-17.5624101671002,
10.1707588393922));
#212617=CARTESIAN_POINT('Ctrl Pts',(21.3604512607793,-20.4647816823687,
10.2979346460737));
#212618=CARTESIAN_POINT('Ctrl Pts',(18.8836382608913,-21.9792698978844,
10.4251104527551));
#212619=CARTESIAN_POINT('Ctrl Pts',(16.2695414442335,-20.7164258756515,
10.5522862594365));
#212620=CARTESIAN_POINT('Ctrl Pts',(15.9164323909425,-17.8348306251289,
10.6794620661178));
#212621=CARTESIAN_POINT('Ctrl Pts',(18.1482667409934,-15.9781689366991,
10.8066378727994));
#212622=CARTESIAN_POINT('Ctrl Pts',(20.9174750014767,-16.8498126720757,
10.9338136794808));
#212623=CARTESIAN_POINT('Ctrl Pts',(21.6834804698477,-19.6500828043623,
11.0609894861623));
#212624=CARTESIAN_POINT('Ctrl Pts',(19.7435206725372,-21.8099052915517,
11.1881652928437));
#212625=CARTESIAN_POINT('Ctrl Pts',(16.8773883160933,-21.3477770553498,
11.315341099525));
#212626=CARTESIAN_POINT('Ctrl Pts',(15.7145819453165,-18.6876720695586,
11.4425169062065));
#212627=CARTESIAN_POINT('Ctrl Pts',(17.321904233492,-16.2700715539058,11.569692712888));
#212628=CARTESIAN_POINT('Ctrl Pts',(20.2247367428907,-16.3129739282918,
11.6968685195694));
#212629=CARTESIAN_POINT('Ctrl Pts',(21.7599108162444,-18.7770189270395,
11.8240443262509));
#212630=CARTESIAN_POINT('Ctrl Pts',(20.5189995249001,-21.4015981996781,
11.9512201329323));
#212631=CARTESIAN_POINT('Ctrl Pts',(17.6404619590251,-21.7788231633232,
12.0783959396136));
#212632=CARTESIAN_POINT('Ctrl Pts',(15.7651776731192,-19.5626133270522,
12.2055717462952));
#212633=CARTESIAN_POINT('Ctrl Pts',(16.6136036062314,-16.7862036621481,
12.3327475529766));
#212634=CARTESIAN_POINT('Ctrl Pts',(19.4073616239837,-15.9967777127422,
12.459923359658));
#212635=CARTESIAN_POINT('Ctrl Pts',(21.5833521452667,-17.9185847901141,
12.5870991663395));
#212636=CARTESIAN_POINT('Ctrl Pts',(21.1452389240066,-20.7884861815747,
12.7142749730209));
#212637=CARTESIAN_POINT('Ctrl Pts',(18.4949636483364,-21.9735254866281,
12.8414507797022));
#212638=CARTESIAN_POINT('Ctrl Pts',(16.0639893890483,-20.3865026947222,
12.9686265863838));
#212639=CARTESIAN_POINT('Ctrl Pts',(16.0825841457601,-17.4834127156872,
13.0958023930652));
#212640=CARTESIAN_POINT('Ctrl Pts',(18.5336883833095,-15.9276604192025,
13.2229781997466));
#212641=CARTESIAN_POINT('Ctrl Pts',(21.1685660964313,-17.1465519764151,
13.3501540064281));
#212642=CARTESIAN_POINT('Ctrl Pts',(21.5698805222909,-20.0218300365248,
13.4773298131095));
#212643=CARTESIAN_POINT('Ctrl Pts',(19.3694505835445,-21.9156054392635,
13.604505619791));
#212644=CARTESIAN_POINT('Ctrl Pts',(16.5860341749072,-21.0904567935765,
13.7316814264724));
#212645=CARTESIAN_POINT('Ctrl Pts',(15.773243092998,-18.3034067673804,13.8588572331538));
#212646=CARTESIAN_POINT('Ctrl Pts',(17.6767627079645,-16.1114007758768,
13.9860330398352));
#212647=CARTESIAN_POINT('Ctrl Pts',(20.5502319188267,-16.5254682650346,
14.1132088465167));
#212648=CARTESIAN_POINT('Ctrl Pts',(21.7574210722316,-19.1657280134782,
14.2403846531981));
#212649=CARTESIAN_POINT('Ctrl Pts',(20.1908090465392,-21.6099055750122,
14.3675604598796));
#212650=CARTESIAN_POINT('Ctrl Pts',(17.2876651404139,-21.6156197396974,
14.494736266561));
#212651=CARTESIAN_POINT('Ctrl Pts',(15.7114436982933,-19.1776281160963,
14.6219120732424));
#212652=CARTESIAN_POINT('Ctrl Pts',(16.9082300619871,-16.532636700037,14.7490878799238));
#212653=CARTESIAN_POINT('Ctrl Pts',(19.7800470237451,-16.1072609490722,
14.8762636866053));
#212654=CARTESIAN_POINT('Ctrl Pts',(21.6921807662175,-18.2917567129154,
15.0034394932867));
#212655=CARTESIAN_POINT('Ctrl Pts',(20.8903672610905,-21.0819847133387,
15.1306152999681));
#212656=CARTESIAN_POINT('Ctrl Pts',(18.1102206331594,-21.9180839410347,
15.2577911066496));
#212657=CARTESIAN_POINT('Ctrl Pts',(15.9023528581907,-20.0329852487628,
15.384966913331));
#212658=CARTESIAN_POINT('Ctrl Pts',(16.2923455839892,-17.1561496842624,
15.5121427200124));
#212659=CARTESIAN_POINT('Ctrl Pts',(18.9224046903134,-15.9268953214099,
15.6393185266939));
#212660=CARTESIAN_POINT('Ctrl Pts',(21.3796141869889,-17.4729867419922,
15.7664943333753));
#212661=CARTESIAN_POINT('Ctrl Pts',(21.4096368724374,-20.375981028881,15.8936701400568));
#212662=CARTESIAN_POINT('Ctrl Pts',(18.9849287961779,-21.9725611040017,
16.0208459467382));
#212663=CARTESIAN_POINT('Ctrl Pts',(16.3300091238228,-20.7979638433666,
16.1480217534196));
#212664=CARTESIAN_POINT('Ctrl Pts',(15.8806018718589,-17.9298093298801,
16.2751975601011));
#212665=CARTESIAN_POINT('Ctrl Pts',(18.0490103006032,-15.9994513119205,
16.4023733667825));
#212666=CARTESIAN_POINT('Ctrl Pts',(20.8458542632885,-16.7778734594348,
16.5295491734639));
#212667=CARTESIAN_POINT('Ctrl Pts',(21.7052030158649,-19.5509217664062,
16.6567249801454));
#212668=CARTESIAN_POINT('Ctrl Pts',(19.8386574150423,-21.7744965259768,
16.7839007868268));
#212669=CARTESIAN_POINT('Ctrl Pts',(16.9586571986901,-21.4086059068554,
16.9110765935082));
#212670=CARTESIAN_POINT('Ctrl Pts',(15.7074238123383,-18.7889318423525,
17.0382524001897));
#212671=CARTESIAN_POINT('Ctrl Pts',(17.2328862276622,-16.3188626913401,
17.1654282068711));
#212672=CARTESIAN_POINT('Ctrl Pts',(20.135527359478,-16.2645335900898,17.2926040135526));
#212673=CARTESIAN_POINT('Ctrl Pts',(21.7523541275707,-18.6757881169556,
17.4197798202339));
#212674=CARTESIAN_POINT('Ctrl Pts',(20.6000283238033,-21.3404499028704,
17.5469556269154));
#212675=CARTESIAN_POINT('Ctrl Pts',(17.7357373517245,-21.8138571468239,
17.6741314335968));
#212676=CARTESIAN_POINT('Ctrl Pts',(15.7872904002738,-19.6616880854488,
17.8013072402783));
#212677=CARTESIAN_POINT('Ctrl Pts',(16.5422666131419,-16.8584242538939,
17.9284830469597));
#212678=CARTESIAN_POINT('Ctrl Pts',(19.3080221741474,-15.9758862274083,
18.0556588536411));
#212679=CARTESIAN_POINT('Ctrl Pts',(21.5471480181857,-17.8237478688561,
18.1828346603226));
#212680=CARTESIAN_POINT('Ctrl Pts',(21.2053851592371,-20.7067108133391,
18.310010467004));
#212681=CARTESIAN_POINT('Ctrl Pts',(18.5962798080717,-21.9798354963434,
18.4371862736854));
#212682=CARTESIAN_POINT('Ctrl Pts',(16.1135241852737,-20.4751090398787,
18.5643620803669));
#212683=CARTESIAN_POINT('Ctrl Pts',(16.0348924771216,-17.5730245745949,
18.6915378870483));
#212684=CARTESIAN_POINT('Ctrl Pts',(18.4325243962693,-15.9360644723642,
18.8187136937297));
#212685=CARTESIAN_POINT('Ctrl Pts',(21.1067414690649,-17.0660380283814,
18.9458895004112));
#212686=CARTESIAN_POINT('Ctrl Pts',(21.6041155150354,-19.9262646340588,
19.0730653070926));
#212687=CARTESIAN_POINT('Ctrl Pts',(19.4683367113789,-21.8926639140248,
19.200241113774));
#212688=CARTESIAN_POINT('Ctrl Pts',(16.6588495608948,-21.1611865588169,
19.3274169204555));
#212689=CARTESIAN_POINT('Ctrl Pts',(15.7531841249269,-18.4029176770637,
19.4545927271369));
#212690=CARTESIAN_POINT('Ctrl Pts',(17.582232272941,-16.148397701268,19.5817685338184));
#212691=CARTESIAN_POINT('Ctrl Pts',(20.4679557680829,-16.4660089109295,
19.7089443404998));
#212692=CARTESIAN_POINT('Ctrl Pts',(21.762882574719,-19.0643624781199,19.8361201471812));
#212693=CARTESIAN_POINT('Ctrl Pts',(20.278997406019,-21.5596307706316,19.9632959538627));
#212694=CARTESIAN_POINT('Ctrl Pts',(17.3776734088588,-21.662559052761,20.0904717605441));
#212695=CARTESIAN_POINT('Ctrl Pts',(15.7206941087448,-19.2787188466078,
20.2176475672255));
#212696=CARTESIAN_POINT('Ctrl Pts',(16.828237415124,-16.5951320529376,20.344823373907));
#212697=CARTESIAN_POINT('Ctrl Pts',(19.6841967603538,-16.0738297948901,
20.4719991805884));
#212698=CARTESIAN_POINT('Ctrl Pts',(21.6684150405127,-18.1930614333217,
20.5991749872697));
#212699=CARTESIAN_POINT('Ctrl Pts',(20.9604790804735,-21.0085887233582,
20.7263507939513));
#212700=CARTESIAN_POINT('Ctrl Pts',(18.2099071212035,-21.9372914819773,
20.8535266006327));
#212701=CARTESIAN_POINT('Ctrl Pts',(15.9401186110067,-20.1272362927054,
20.9807024073141));
#212702=CARTESIAN_POINT('Ctrl Pts',(16.2336184655874,-17.2388558767421,
21.1078782139956));
#212703=CARTESIAN_POINT('Ctrl Pts',(18.8209175351634,-15.9224078905259,
21.2350540206769));
#212704=CARTESIAN_POINT('Ctrl Pts',(21.3287557911663,-17.3849813380486,
21.3622298273584));
#212705=CARTESIAN_POINT('Ctrl Pts',(21.4555258683986,-20.286047713047,21.4894056340398));
#212706=CARTESIAN_POINT('Ctrl Pts',(19.0865078830173,-21.9615659646048,
21.6165814407213));
#212707=CARTESIAN_POINT('Ctrl Pts',(16.3920659006521,-20.879190353892,21.7437572474027));
#212708=CARTESIAN_POINT('Ctrl Pts',(15.8501931440795,-18.0222746586101,
21.8709330540842));
#212709=CARTESIAN_POINT('Ctrl Pts',(17.2469900335074,-16.6964452121458,
21.9557169252051));
#212710=CARTESIAN_POINT('Ctrl Pts',(18.0714160310384,-16.4758408723594,
21.9981088607656));
#212711=CARTESIAN_POINT('Ctrl Pts',(20.3539256943887,-17.5890877707427,
-4.33680868994202E-19));
#212712=CARTESIAN_POINT('Ctrl Pts',(20.4076089239479,-17.6408883813468,
1.14879278225653E-14));
#212713=CARTESIAN_POINT('Ctrl Pts',(20.4581355958119,-17.6955615793788,
3.22355904239226E-15));
#212714=CARTESIAN_POINT('Ctrl Pts',(20.505511977026,-17.7527360595703,3.08607306376274E-15));
#212715=CARTESIAN_POINT('Ctrl Pts',(20.5545756607811,-17.8119468000931,
2.94369054311896E-15));
#212716=CARTESIAN_POINT('Ctrl Pts',(20.6002611686401,-17.873840595982,1.23841336720853E-14));
#212717=CARTESIAN_POINT('Ctrl Pts',(20.6425471220966,-17.9380546484764,
1.20702059458466E-14));
#212718=CARTESIAN_POINT('Ctrl Pts',(20.6826816235519,-17.9990015770098,
1.17722504368497E-14));
#212719=CARTESIAN_POINT('Ctrl Pts',(20.7197537535956,-18.0620396014582,
1.56295612152767E-14));
#212720=CARTESIAN_POINT('Ctrl Pts',(20.7537167666138,-18.1268912820608,
3.65679708735911E-15));
#212721=CARTESIAN_POINT('Ctrl Pts',(20.7688150878339,-18.1557212184648,
-1.85535512480841E-15));
#212722=CARTESIAN_POINT('Ctrl Pts',(20.7832985724702,-18.1849099468526,
-9.481700208412E-17));
#212723=CARTESIAN_POINT('Ctrl Pts',(20.7971611207678,-18.2144346312911,
-4.68375338513738E-15));
#212724=CARTESIAN_POINT('Ctrl Pts',(20.8057380545325,-18.2327019265545,
-7.25563266417811E-15));
#212725=CARTESIAN_POINT('Ctrl Pts',(20.8140776656103,-18.2510987616938,
5.43075649196809E-15));
#212726=CARTESIAN_POINT('Ctrl Pts',(20.8221770088969,-18.269617013417,1.47659662275146E-14));
#212727=CARTESIAN_POINT('Ctrl Pts',(20.8264660877165,-18.2794235172817,
1.97095090477139E-14));
#212728=CARTESIAN_POINT('Ctrl Pts',(20.8306870781385,-18.2892625308288,
2.34250044198635E-14));
#212729=CARTESIAN_POINT('Ctrl Pts',(20.8348368140281,-18.2991258749815,
2.40155118014229E-14));
#212730=CARTESIAN_POINT('Ctrl Pts',(20.8659056770803,-18.372972234574,2.92160735740311E-14));
#212731=CARTESIAN_POINT('Ctrl Pts',(20.8930393303568,-18.4483069573626,
1.37453420125155E-14));
#212732=CARTESIAN_POINT('Ctrl Pts',(20.9162161420459,-18.5247489058203,
2.05252481677576E-14));
#212733=CARTESIAN_POINT('Ctrl Pts',(20.9398193164082,-18.6025970871082,
2.74298780749852E-14));
#212734=CARTESIAN_POINT('Ctrl Pts',(20.9593192432915,-18.6815944151039,
-7.79267749674098E-15));
#212735=CARTESIAN_POINT('Ctrl Pts',(20.9746521798114,-18.7613738906736,
2.88657986402541E-15));
#212736=CARTESIAN_POINT('Ctrl Pts',(20.9885844406082,-18.8338654488575,
1.25902787264266E-14));
#212737=CARTESIAN_POINT('Ctrl Pts',(20.9990759862006,-18.9070037360458,
7.24757628038241E-15));
#212738=CARTESIAN_POINT('Ctrl Pts',(21.0060452061984,-18.9805292501327,
6.84174938925253E-15));
#212739=CARTESIAN_POINT('Ctrl Pts',(21.0087031403799,-19.0085705484655,
6.67475528854553E-15));
#212740=CARTESIAN_POINT('Ctrl Pts',(21.0108483899423,-19.0366682762212,
1.44685164024077E-15));
#212741=CARTESIAN_POINT('Ctrl Pts',(21.0124750673575,-19.0648083237754,
9.10382880192628E-15));
#212742=CARTESIAN_POINT('Ctrl Pts',(21.0133685834701,-19.0802653441188,
1.32694517658755E-14));
#212743=CARTESIAN_POINT('Ctrl Pts',(21.014105623128,-19.0957351348357,1.68885348715346E-14));
#212744=CARTESIAN_POINT('Ctrl Pts',(21.0146851084115,-19.1112153648711,
-3.7470027081099E-15));
#212745=CARTESIAN_POINT('Ctrl Pts',(21.0151328224698,-19.1231754901941,
-2.01423518057422E-14));
#212746=CARTESIAN_POINT('Ctrl Pts',(21.0154863189935,-19.1351385470168,
5.5845216903151E-15));
#212747=CARTESIAN_POINT('Ctrl Pts',(21.0157451770828,-19.1470949182306,
6.34214902817121E-15));
#212748=CARTESIAN_POINT('Ctrl Pts',(21.0175519249061,-19.2305466184455,
1.17423994501049E-14));
#212749=CARTESIAN_POINT('Ctrl Pts',(21.0147568373932,-19.3137920798114,
-1.49327707601934E-14));
#212750=CARTESIAN_POINT('Ctrl Pts',(21.0073036695044,-19.3964506692726,
-1.12410081243297E-14));
#212751=CARTESIAN_POINT('Ctrl Pts',(20.9998648261745,-19.4789503936919,
-7.14671687260285E-15));
#212752=CARTESIAN_POINT('Ctrl Pts',(20.9877861648147,-19.5608665038776,
-8.09133270479139E-15));
#212753=CARTESIAN_POINT('Ctrl Pts',(20.9709624036051,-19.6418361818354,
-1.15740750317173E-14));
#212754=CARTESIAN_POINT('Ctrl Pts',(20.9545246825771,-19.7209479191819,
-1.49826315955414E-14));
#212755=CARTESIAN_POINT('Ctrl Pts',(20.9335573448041,-19.799157111958,-9.03506803208643E-15));
#212756=CARTESIAN_POINT('Ctrl Pts',(20.9083260528412,-19.8762372781696,
-1.765254609154E-14));
#212757=CARTESIAN_POINT('Ctrl Pts',(20.8979286223519,-19.9080008387303,
-2.11749609793981E-14));
#212758=CARTESIAN_POINT('Ctrl Pts',(20.886806496403,-19.9395726045308,-6.78433755510298E-15));
#212759=CARTESIAN_POINT('Ctrl Pts',(20.8749757808311,-19.9709362516545,
5.4678483962789E-15));
#212760=CARTESIAN_POINT('Ctrl Pts',(20.8684245113494,-19.9883038997047,
1.2315661009052E-14));
#212761=CARTESIAN_POINT('Ctrl Pts',(20.8616537141196,-20.0056128698145,
-8.32710061231184E-15));
#212762=CARTESIAN_POINT('Ctrl Pts',(20.8546785166995,-20.0228303119358,
-5.13478148889135E-15));
#212763=CARTESIAN_POINT('Ctrl Pts',(20.8236218670382,-20.0994899440325,
8.84067847874355E-15));
#212764=CARTESIAN_POINT('Ctrl Pts',(20.7884837604207,-20.1744320701159,
2.95709367352313E-15));
#212765=CARTESIAN_POINT('Ctrl Pts',(20.7495952387339,-20.247430956818,1.0019762797242E-14));
#212766=CARTESIAN_POINT('Ctrl Pts',(20.7099066604874,-20.3219316552531,
1.72277327582215E-14));
#212767=CARTESIAN_POINT('Ctrl Pts',(20.6663114480379,-20.3944090798839,
-1.83234150877214E-14));
#212768=CARTESIAN_POINT('Ctrl Pts',(20.6191066061375,-20.4646182429735,
-4.46864767411626E-15));
#212769=CARTESIAN_POINT('Ctrl Pts',(20.571128607974,-20.535977344332,9.61304349920823E-15));
#212770=CARTESIAN_POINT('Ctrl Pts',(20.5194213554847,-20.6049941328661,
2.46291640853547E-15));
#212771=CARTESIAN_POINT('Ctrl Pts',(20.4642461984926,-20.6713939737934,
-2.96984659087229E-15));
#212772=CARTESIAN_POINT('Ctrl Pts',(20.440364318256,-20.7001343188184,-5.32135046289197E-15));
#212773=CARTESIAN_POINT('Ctrl Pts',(20.4158321356603,-20.7283840869128,
-6.72565667072835E-15));
#212774=CARTESIAN_POINT('Ctrl Pts',(20.3906682941055,-20.7561193805442,
-3.1641356201817E-15));
#212775=CARTESIAN_POINT('Ctrl Pts',(20.3815365270621,-20.7661843080224,
-1.76561806683548E-15));
#212776=CARTESIAN_POINT('Ctrl Pts',(20.3723208078371,-20.7761822779911,
4.05228345890246E-16));
#212777=CARTESIAN_POINT('Ctrl Pts',(20.3630243316464,-20.7861096027615,
-2.22044604925031E-16));
#212778=CARTESIAN_POINT('Ctrl Pts',(20.3025147033051,-20.8507253474758,
-4.84969820433169E-15));
#212779=CARTESIAN_POINT('Ctrl Pts',(20.2387852854453,-20.9121400047012,
-1.86639630302913E-14));
#212780=CARTESIAN_POINT('Ctrl Pts',(20.1721441659296,-20.9700792099884,
-2.05391259555654E-14));
#212781=CARTESIAN_POINT('Ctrl Pts',(20.1169512585411,-21.0180650964023,
-2.20921564932416E-14));
#212782=CARTESIAN_POINT('Ctrl Pts',(20.0597599950038,-21.0636670219304,
-1.76874795853289E-14));
#212783=CARTESIAN_POINT('Ctrl Pts',(20.0007222397457,-21.1067151539364,
-1.05748743095546E-14));
#212784=CARTESIAN_POINT('Ctrl Pts',(19.9812253420094,-21.1209315655156,
-8.39014400518185E-15));
#212785=CARTESIAN_POINT('Ctrl Pts',(19.9615269106471,-21.1348693297411,
1.57955388576365E-14));
#212786=CARTESIAN_POINT('Ctrl Pts',(19.941631987048,-21.1485219218181,5.80091530366644E-15));
#212787=CARTESIAN_POINT('Ctrl Pts',(19.9257068710437,-21.1594502931437,
-2.07749129685265E-15));
#212788=CARTESIAN_POINT('Ctrl Pts',(19.9096544895287,-21.170196697329,-1.40009963692834E-14));
#212789=CARTESIAN_POINT('Ctrl Pts',(19.8934933729568,-21.1807476067171,
-1.42386102908176E-14));
#212790=CARTESIAN_POINT('Ctrl Pts',(19.8189655561075,-21.2294036657816,
-1.49307265937708E-14));
#212791=CARTESIAN_POINT('Ctrl Pts',(19.7420556060774,-21.2739560343907,
-1.3588777424594E-14));
#212792=CARTESIAN_POINT('Ctrl Pts',(19.6630443896218,-21.3141141071315,
-1.16295861829485E-14));
#212793=CARTESIAN_POINT('Ctrl Pts',(19.585203146919,-21.3536775315024,-9.64882108030855E-15));
#212794=CARTESIAN_POINT('Ctrl Pts',(19.5053217267533,-21.3889765584864,
-2.19053443386609E-14));
#212795=CARTESIAN_POINT('Ctrl Pts',(19.4236362626317,-21.4196959407397,
-5.55111512312578E-17));
#212796=CARTESIAN_POINT('Ctrl Pts',(19.4149414973774,-21.4229657736325,
2.2126898693708E-15));
#212797=CARTESIAN_POINT('Ctrl Pts',(19.4062262673531,-21.4261836782215,
-3.67255004627579E-14));
#212798=CARTESIAN_POINT('Ctrl Pts',(19.3974909880357,-21.4293497847436,
-2.27595720048157E-15));
#212799=CARTESIAN_POINT('Ctrl Pts',(18.0714161019496,-21.428158862637,0.00189098085166763));
#212800=CARTESIAN_POINT('Ctrl Pts',(17.2469901926503,-21.2075545464601,
0.0442829164121458));
#212801=CARTESIAN_POINT('Ctrl Pts',(15.8501939821074,-19.8817220316731,
0.129066787533101));
#212802=CARTESIAN_POINT('Ctrl Pts',(16.3920656827787,-17.0248116182672,
0.256242594214536));
#212803=CARTESIAN_POINT('Ctrl Pts',(19.0865079334355,-15.9424330181619,
0.38341840089597));
#212804=CARTESIAN_POINT('Ctrl Pts',(21.4555257912919,-17.6179530146914,
0.510594207577404));
#212805=CARTESIAN_POINT('Ctrl Pts',(21.3287556480917,-20.5190182015967,
0.63777001425884));
#212806=CARTESIAN_POINT('Ctrl Pts',(18.8209175719769,-21.9815922294721,
0.764945820940273));
#212807=CARTESIAN_POINT('Ctrl Pts',(16.2336185304982,-20.6651439233068,
0.892121627621708));
#212808=CARTESIAN_POINT('Ctrl Pts',(15.9401187363004,-17.7767638289518,
1.01929743430314));
#212809=CARTESIAN_POINT('Ctrl Pts',(18.2099071283678,-15.9667085869429,
1.14647324098458));
#212810=CARTESIAN_POINT('Ctrl Pts',(20.9604790041794,-16.8954113789202,
1.27364904766601));
#212811=CARTESIAN_POINT('Ctrl Pts',(21.6684149250655,-19.7109385242504,
1.40082485434745));
#212812=CARTESIAN_POINT('Ctrl Pts',(19.6841967272255,-21.8301701041092,
1.52800066102888));
#212813=CARTESIAN_POINT('Ctrl Pts',(16.8282374854801,-21.3088678538367,
1.65517646771032));
#212814=CARTESIAN_POINT('Ctrl Pts',(15.720694223426,-18.6252811680681,1.78235227439175));
#212815=CARTESIAN_POINT('Ctrl Pts',(17.3776734595451,-16.2414410482877,
1.90952808107318));
#212816=CARTESIAN_POINT('Ctrl Pts',(20.2789973479827,-16.3443693285228,
2.03670388775462));
#212817=CARTESIAN_POINT('Ctrl Pts',(21.7628824602006,-18.839637525737,2.16387969443605));
#212818=CARTESIAN_POINT('Ctrl Pts',(20.4679557027106,-21.4379909954235,
2.29105550111749));
#212819=CARTESIAN_POINT('Ctrl Pts',(17.5822323163742,-21.7556021927696,
2.41823130779892));
#212820=CARTESIAN_POINT('Ctrl Pts',(15.7531842374939,-19.5010823022681,
2.54540711448036));
#212821=CARTESIAN_POINT('Ctrl Pts',(16.6588496392251,-16.7428135245559,
2.67258292116179));
#212822=CARTESIAN_POINT('Ctrl Pts',(19.468336683663,-16.0113361970163,2.79975872784322));
#212823=CARTESIAN_POINT('Ctrl Pts',(21.6041154066714,-17.977735402714,2.92693453452466));
#212824=CARTESIAN_POINT('Ctrl Pts',(21.1067413794861,-20.8379619004206,
3.05411034120609));
#212825=CARTESIAN_POINT('Ctrl Pts',(18.43252440765,-21.9679354137682,3.18128614788753));
#212826=CARTESIAN_POINT('Ctrl Pts',(16.0348925790254,-20.3309753733442,
3.30846195456896));
#212827=CARTESIAN_POINT('Ctrl Pts',(16.1135242842076,-17.4288910176245,
3.43563776125039));
#212828=CARTESIAN_POINT('Ctrl Pts',(18.5962798132715,-15.924164617971,3.56281356793183));
#212829=CARTESIAN_POINT('Ctrl Pts',(21.2053850659314,-17.1972892529086,
3.68998937461327));
#212830=CARTESIAN_POINT('Ctrl Pts',(21.5471479119772,-20.0802520885476,
3.8171651812947));
#212831=CARTESIAN_POINT('Ctrl Pts',(19.3080221524756,-21.9281136602303,
3.94434098797614));
#212832=CARTESIAN_POINT('Ctrl Pts',(16.5422666958893,-21.0455756670647,
4.07151679465757));
#212833=CARTESIAN_POINT('Ctrl Pts',(15.7872905115249,-18.242311941345,4.198692601339));
#212834=CARTESIAN_POINT('Ctrl Pts',(17.7357373894132,-16.0901429612237,
4.32586840802044));
#212835=CARTESIAN_POINT('Ctrl Pts',(20.6000282533525,-16.5635501873038,
4.45304421470187));
#212836=CARTESIAN_POINT('Ctrl Pts',(21.7523540136146,-19.2282118726162,
4.5802200213833));
#212837=CARTESIAN_POINT('Ctrl Pts',(20.1355273065643,-21.6394663084466,
4.70739582806474));
#212838=CARTESIAN_POINT('Ctrl Pts',(17.2328862843358,-21.5851372092476,
4.83457163474617));
#212839=CARTESIAN_POINT('Ctrl Pts',(15.7074239266047,-19.115068151491,4.96174744142761));
#212840=CARTESIAN_POINT('Ctrl Pts',(16.9586572657169,-16.4953941858922,
5.08892324810904));
#212841=CARTESIAN_POINT('Ctrl Pts',(19.8386573733367,-16.1295035805846,
5.21609905479048));
#212842=CARTESIAN_POINT('Ctrl Pts',(21.705202903689,-18.3530782562058,5.34327486147191));
#212843=CARTESIAN_POINT('Ctrl Pts',(20.8458541835568,-21.1261264584823,
5.47045066815334));
#212844=CARTESIAN_POINT('Ctrl Pts',(18.0490103264645,-21.9045485766079,
5.59762647483478));
#212845=CARTESIAN_POINT('Ctrl Pts',(15.8806019795871,-19.9741906315278,
5.72480228151621));
#212846=CARTESIAN_POINT('Ctrl Pts',(16.3300092145838,-17.1060362263267,
5.85197808819766));
#212847=CARTESIAN_POINT('Ctrl Pts',(18.9849287867042,-15.9314390100375,
5.97915389487907));
#212848=CARTESIAN_POINT('Ctrl Pts',(21.4096367714204,-17.5280190248805,
6.10632970156052));
#212849=CARTESIAN_POINT('Ctrl Pts',(21.3796140871054,-20.4310132021685,
6.23350550824194));
#212850=CARTESIAN_POINT('Ctrl Pts',(18.9224046832003,-21.9771045643792,
6.36068131492339));
#212851=CARTESIAN_POINT('Ctrl Pts',(16.2923456761723,-20.7478502479364,
6.48785712160482));
#212852=CARTESIAN_POINT('Ctrl Pts',(15.9023529650977,-17.8710147920491,
6.61503292828625));
#212853=CARTESIAN_POINT('Ctrl Pts',(18.1102206567097,-15.9859161709479,
6.74220873496769));
#212854=CARTESIAN_POINT('Ctrl Pts',(20.8903671796782,-16.8220153670774,
6.86938454164913));
#212855=CARTESIAN_POINT('Ctrl Pts',(21.6921806545333,-19.6122432621575,
6.99656034833056));
#212856=CARTESIAN_POINT('Ctrl Pts',(19.7800469842523,-21.7967389435265,
7.12373615501199));
#212857=CARTESIAN_POINT('Ctrl Pts',(16.9082301309179,-21.3713632086215,
7.25091196169343));
#212858=CARTESIAN_POINT('Ctrl Pts',(15.711443812408,-18.7263718924222,7.37808776837486));
#212859=CARTESIAN_POINT('Ctrl Pts',(17.2876651950193,-16.2883803608658,
7.5052635750563));
#212860=CARTESIAN_POINT('Ctrl Pts',(20.1908089915383,-16.2940945253353,
7.63243938173773));
#212861=CARTESIAN_POINT('Ctrl Pts',(21.7574209580843,-18.7382719945909,
7.75961518841917));
#212862=CARTESIAN_POINT('Ctrl Pts',(20.5502318502561,-21.3785316433533,
7.8867909951006));
#212863=CARTESIAN_POINT('Ctrl Pts',(17.6767627478799,-21.7925991168781,
8.01396680178203));
#212864=CARTESIAN_POINT('Ctrl Pts',(15.7732432047795,-19.6005932081323,
8.14114260846348));
#212865=CARTESIAN_POINT('Ctrl Pts',(16.5860342560023,-16.8135432871596,
8.26831841514489));
#212866=CARTESIAN_POINT('Ctrl Pts',(19.3694505595535,-15.9883946726254,
8.39549422182634));
#212867=CARTESIAN_POINT('Ctrl Pts',(21.5698804152241,-17.8821700038661,
8.52267002850777));
#212868=CARTESIAN_POINT('Ctrl Pts',(21.1685660045158,-20.7574479554213,
8.6498458351892));
#212869=CARTESIAN_POINT('Ctrl Pts',(18.5336883908723,-21.9763394666155,
8.77702164187065));
#212870=CARTESIAN_POINT('Ctrl Pts',(16.0825842458626,-20.4205872288672,
8.90419744855206));
#212871=CARTESIAN_POINT('Ctrl Pts',(16.0639894898528,-17.5174973594366,
9.03137325523352));
#212872=CARTESIAN_POINT('Ctrl Pts',(18.4949636573611,-15.9304746274477,
9.15854906191495));
#212873=CARTESIAN_POINT('Ctrl Pts',(21.1452388329719,-17.1155138877607,
9.28572486859637));
#212874=CARTESIAN_POINT('Ctrl Pts',(21.5833520376912,-19.98541517087,9.4129006752778));
#212875=CARTESIAN_POINT('Ctrl Pts',(19.4073615985613,-21.9072221756853,
9.54007648195925));
#212876=CARTESIAN_POINT('Ctrl Pts',(16.6136036862856,-21.1177962560837,
9.66725228864067));
#212877=CARTESIAN_POINT('Ctrl Pts',(15.7651777852051,-18.3413866960012,
9.79442809532212));
#212878=CARTESIAN_POINT('Ctrl Pts',(17.6404620003109,-16.1251769434017,
9.92160390200354));
#212879=CARTESIAN_POINT('Ctrl Pts',(20.5189994575086,-16.5024018928049,
10.048779708685));
#212880=CARTESIAN_POINT('Ctrl Pts',(21.7599107020031,-19.1269810663543,
10.1759555153665));
#212881=CARTESIAN_POINT('Ctrl Pts',(20.2247366866089,-21.5910259720733,
10.3031313220479));
#212882=CARTESIAN_POINT('Ctrl Pts',(17.3219042868047,-21.6339283448398,
10.4303071287293));
#212883=CARTESIAN_POINT('Ctrl Pts',(15.7145820593127,-19.2163279204619,
10.5574829354107));
#212884=CARTESIAN_POINT('Ctrl Pts',(16.8773883861884,-16.5562230351012,
10.6846587420922));
#212885=CARTESIAN_POINT('Ctrl Pts',(19.7435206344235,-16.0940948163466,
10.8118345487736));
#212886=CARTESIAN_POINT('Ctrl Pts',(21.683480358492,-18.2539172219934,10.9390103554551));
#212887=CARTESIAN_POINT('Ctrl Pts',(20.9174749190411,-21.0541872485576,
11.0661861621365));
#212888=CARTESIAN_POINT('Ctrl Pts',(18.1482667631075,-21.9258309510259,
11.1933619688179));
#212889=CARTESIAN_POINT('Ctrl Pts',(15.9164324973179,-20.069169332693,11.3205377754993));
#212890=CARTESIAN_POINT('Ctrl Pts',(16.2695415372774,-17.1875741909633,
11.4477135821808));
#212891=CARTESIAN_POINT('Ctrl Pts',(18.8836382552418,-15.9247302164082,
11.5748893888622));
#212892=CARTESIAN_POINT('Ctrl Pts',(21.3604511616193,-17.4392183747454,
11.7020651955437));
#212893=CARTESIAN_POINT('Ctrl Pts',(21.427658143155,-20.3415897804367,11.8292410022251));
#212894=CARTESIAN_POINT('Ctrl Pts',(19.0236009656254,-21.9690988102461,
11.9564168089065));
#212895=CARTESIAN_POINT('Ctrl Pts',(16.3538528767977,-20.828606943926,12.083592615588));
#212896=CARTESIAN_POINT('Ctrl Pts',(15.8677420449167,-17.9664446819167,
12.2107684222694));
#212897=CARTESIAN_POINT('Ctrl Pts',(18.0112449867927,-16.008468253787,12.3379442289508));
#212898=CARTESIAN_POINT('Ctrl Pts',(20.817830794051,-16.7509995066233,12.4651200356323));
#212899=CARTESIAN_POINT('Ctrl Pts',(21.712631184893,-19.5128121026353,12.5922958423137));
#212900=CARTESIAN_POINT('Ctrl Pts',(19.874722338297,-21.7601144024042,12.7194716489951));
#212901=CARTESIAN_POINT('Ctrl Pts',(16.9902715475267,-21.4311460292034,
12.8466474556766));
#212902=CARTESIAN_POINT('Ctrl Pts',(15.7055833839069,-18.8277150473647,
12.973823262358));
#212903=CARTESIAN_POINT('Ctrl Pts',(17.1992795008189,-16.3383077955748,
13.1009990690394));
#212904=CARTESIAN_POINT('Ctrl Pts',(20.1009864202325,-16.2468009173113,
13.2281748757209));
#212905=CARTESIAN_POINT('Ctrl Pts',(21.7485681438287,-18.6371462938237,
13.3553506824023));
#212906=CARTESIAN_POINT('Ctrl Pts',(20.6304707006625,-21.3163504037278,
13.4825264890837));
#212907=CARTESIAN_POINT('Ctrl Pts',(17.7724790978853,-21.8264097663479,
13.6097022957652));
#212908=CARTESIAN_POINT('Ctrl Pts',(15.7966232440805,-19.6993765743343,
13.7368781024466));
#212909=CARTESIAN_POINT('Ctrl Pts',(16.5156282496692,-16.8866717627907,
13.864053909128));
#212910=CARTESIAN_POINT('Ctrl Pts',(19.2698516485073,-15.9687774201593,
13.9912297158095));
#212911=CARTESIAN_POINT('Ctrl Pts',(21.532464418544,-17.7878046348562,14.1184055224909));
#212912=CARTESIAN_POINT('Ctrl Pts',(21.2276597768573,-20.674908838959,14.2455813291723));
#212913=CARTESIAN_POINT('Ctrl Pts',(18.6350770638849,-21.9813511190996,
14.3727571358538));
#212914=CARTESIAN_POINT('Ctrl Pts',(16.1332500049482,-20.5085517702016,
14.4999329425352));
#212915=CARTESIAN_POINT('Ctrl Pts',(16.0174496457219,-17.6077127826422,
14.6271087492167));
#212916=CARTESIAN_POINT('Ctrl Pts',(18.3939156284153,-15.940173881134,14.7542845558981));
#212917=CARTESIAN_POINT('Ctrl Pts',(21.082387914021,-17.0357985086741,14.8814603625795));
#212918=CARTESIAN_POINT('Ctrl Pts',(21.6163600459046,-19.889419071628,15.008636169261));
#212919=CARTESIAN_POINT('Ctrl Pts',(19.5059457351114,-21.8830158191527,
15.1358119759424));
#212920=CARTESIAN_POINT('Ctrl Pts',(16.6873191247092,-21.1875874719631,
15.2629877826238));
#212921=CARTESIAN_POINT('Ctrl Pts',(15.7463951860447,-18.4411463754548,
15.3901635893052));
#212922=CARTESIAN_POINT('Ctrl Pts',(17.5464132325167,-16.1633817723147,
15.5173393959867));
#212923=CARTESIAN_POINT('Ctrl Pts',(20.4359684282068,-16.4440013119089,
15.6445152026681));
#212924=CARTESIAN_POINT('Ctrl Pts',(21.7640732270913,-19.0255539838723,
15.7716910093496));
#212925=CARTESIAN_POINT('Ctrl Pts',(20.3122739076741,-21.539625440908,15.898866816031));
#212926=CARTESIAN_POINT('Ctrl Pts',(17.4125062366922,-21.6797111620585,
16.0260426227124));
#212927=CARTESIAN_POINT('Ctrl Pts',(15.725127072392,-19.3172911928685,16.1532184293939));
#212928=CARTESIAN_POINT('Ctrl Pts',(16.7982020674565,-16.6197392267502,
16.2803942360753));
#212929=CARTESIAN_POINT('Ctrl Pts',(19.6472515164596,-16.0618917636594,
16.4075700427567));
#212930=CARTESIAN_POINT('Ctrl Pts',(21.6584493818928,-18.1555392270637,
16.5347458494382));
#212931=CARTESIAN_POINT('Ctrl Pts',(20.9866464512386,-20.9798900157063,
16.6619216561196));
#212932=CARTESIAN_POINT('Ctrl Pts',(18.24818021658,-21.9437775799877,16.789097462801));
#212933=CARTESIAN_POINT('Ctrl Pts',(15.9554234798327,-20.162894905289,16.9162732694825));
#212934=CARTESIAN_POINT('Ctrl Pts',(16.2118382424305,-17.2710913116015,
17.0434490761639));
#212935=CARTESIAN_POINT('Ctrl Pts',(18.7821798745847,-15.9214171105603,
17.1706248828453));
#212936=CARTESIAN_POINT('Ctrl Pts',(21.3083194621878,-17.3521146113923,
17.2978006895268));
#212937=CARTESIAN_POINT('Ctrl Pts',(21.4726807235191,-20.2506076561855,
17.4249764962082));
#212938=CARTESIAN_POINT('Ctrl Pts',(19.1244724027178,-21.9577087771101,
17.5521523028896));
#212939=CARTESIAN_POINT('Ctrl Pts',(16.4180298878732,-20.9072586503617,
17.6793281095711));
#212940=CARTESIAN_POINT('Ctrl Pts',(15.8363462055885,-18.0629800689462,
17.8065039162525));
#212941=CARTESIAN_POINT('Ctrl Pts',(17.9130800309984,-16.0343220954698,
17.9336797229339));
#212942=CARTESIAN_POINT('Ctrl Pts',(20.7429569759279,-16.6824525078913,
18.0608555296154));
#212943=CARTESIAN_POINT('Ctrl Pts',(21.7297405853753,-19.412751880308,18.1880313362968));
#212944=CARTESIAN_POINT('Ctrl Pts',(19.9681181443722,-21.7203400000494,
18.3152071429782));
#212945=CARTESIAN_POINT('Ctrl Pts',(17.0742689039165,-21.4881479922645,
18.4423829496597));
#212946=CARTESIAN_POINT('Ctrl Pts',(15.7031199295909,-18.9291976127498,
18.5695587563411));
#212947=CARTESIAN_POINT('Ctrl Pts',(17.1126153022265,-16.3911670081152,
18.6967345630226));
#212948=CARTESIAN_POINT('Ctrl Pts',(20.0096305005975,-16.2025417305957,
18.823910369704));
#212949=CARTESIAN_POINT('Ctrl Pts',(21.7363338892051,-18.5363737640858,
18.9510861763854));
#212950=CARTESIAN_POINT('Ctrl Pts',(20.7085822803688,-21.2515170733997,
19.0782619830668));
#212951=CARTESIAN_POINT('Ctrl Pts',(17.8692739856059,-21.8569961899794,
19.2054377897483));
#212952=CARTESIAN_POINT('Ctrl Pts',(15.8232981382665,-19.7973216105359,
19.3326135964297));
#212953=CARTESIAN_POINT('Ctrl Pts',(16.4477105902148,-16.9621169125157,
19.4597894031112));
#212954=CARTESIAN_POINT('Ctrl Pts',(19.1696516731346,-15.9525064556156,
19.5869652097926));
#212955=CARTESIAN_POINT('Ctrl Pts',(21.4919093843545,-17.6947451283222,
19.714141016474));
#212956=CARTESIAN_POINT('Ctrl Pts',(21.2839564128859,-20.5904371653283,
19.8413168231554));
#212957=CARTESIAN_POINT('Ctrl Pts',(18.7365766963153,-21.9829646927876,
19.9684926298369));
#212958=CARTESIAN_POINT('Ctrl Pts',(16.1868330293274,-20.5947704364421,
20.0956684365183));
#212959=CARTESIAN_POINT('Ctrl Pts',(15.9739569464928,-17.6994358831224,
20.2228442431997));
#212960=CARTESIAN_POINT('Ctrl Pts',(18.2932490893143,-15.9532519029135,
20.3500200498812));
#212961=CARTESIAN_POINT('Ctrl Pts',(21.0169027756026,-16.9582317548374,
20.4771958565626));
#212962=CARTESIAN_POINT('Ctrl Pts',(21.6461349757523,-19.7923729679124,
20.6043716632441));
#212963=CARTESIAN_POINT('Ctrl Pts',(19.6036638566053,-21.8555188556529,
20.7315474699255));
#212964=CARTESIAN_POINT('Ctrl Pts',(16.7633305629729,-21.2548765937423,
20.8587232766069));
#212965=CARTESIAN_POINT('Ctrl Pts',(15.7309633230734,-18.5414683575651,
20.9858990832884));
#212966=CARTESIAN_POINT('Ctrl Pts',(17.4536974658068,-16.2047352548569,
21.1130748899698));
#212967=CARTESIAN_POINT('Ctrl Pts',(20.3510265953171,-16.3883741373928,
21.2402506966512));
#212968=CARTESIAN_POINT('Ctrl Pts',(21.7648402074573,-18.9241211217718,
21.3674265033327));
#212969=CARTESIAN_POINT('Ctrl Pts',(20.3980344426769,-21.4851745132896,
21.4946023100141));
#212970=CARTESIAN_POINT('Ctrl Pts',(17.5046027271422,-21.7227192681557,
21.6217781166956));
#212971=CARTESIAN_POINT('Ctrl Pts',(15.7390234877918,-19.4172952643212,
21.748953923377));
#212972=CARTESIAN_POINT('Ctrl Pts',(16.7212336413073,-16.6869333681719,
21.8761297300584));
#212973=CARTESIAN_POINT('Ctrl Pts',(19.5498595326579,-16.0308555962028,
22.0033055367398));
#212974=CARTESIAN_POINT('Ctrl Pts',(21.6307164666946,-18.0626227175078,
22.1305000010223));
#212975=CARTESIAN_POINT('Ctrl Pts',(21.244679026905,-19.9500078602896,22.2153025297443));
#212976=CARTESIAN_POINT('Ctrl Pts',(20.6946893042483,-20.6030837310342,
22.2577131229058));
#212977=CARTESIAN_POINT('Ctrl Pts',(18.1101968702393,-21.2832302832024,
-0.084727418129243));
#212978=CARTESIAN_POINT('Ctrl Pts',(17.3340242768668,-21.0755378486675,
-0.0423354825687649));
#212979=CARTESIAN_POINT('Ctrl Pts',(16.0189819851084,-19.8273057761765,
0.0424483885521913));
#212980=CARTESIAN_POINT('Ctrl Pts',(16.5291381537116,-17.1376091768898,
0.169624195233626));
#212981=CARTESIAN_POINT('Ctrl Pts',(19.0658757862808,-16.118581759655,0.29680000191506));
#212982=CARTESIAN_POINT('Ctrl Pts',(21.2962359844956,-17.6960342466338,
0.423975808596494));
#212983=CARTESIAN_POINT('Ctrl Pts',(21.1768856466422,-20.4273012583374,
0.551151615277929));
#212984=CARTESIAN_POINT('Ctrl Pts',(18.8158303215486,-21.8042714183123,
0.678327421959364));
#212985=CARTESIAN_POINT('Ctrl Pts',(16.379964849342,-20.5648743004978,0.805503228640797));
#212986=CARTESIAN_POINT('Ctrl Pts',(16.103643479711,-17.8455499279943,0.932679035322232));
#212987=CARTESIAN_POINT('Ctrl Pts',(18.2405820727437,-16.1414364891873,
1.05985484200366));
#212988=CARTESIAN_POINT('Ctrl Pts',(20.8301640861484,-17.0157826813563,
1.1870306486851));
#212989=CARTESIAN_POINT('Ctrl Pts',(21.4966648031415,-19.6665181585552,
1.31420645536653));
#212990=CARTESIAN_POINT('Ctrl Pts',(19.6285820960571,-21.6617119688685,
1.44138226204797));
#212991=CARTESIAN_POINT('Ctrl Pts',(16.9397809967372,-21.1709213290295,
1.5685580687294));
#212992=CARTESIAN_POINT('Ctrl Pts',(15.897061795067,-18.6444038895142,1.69573387541083));
#212993=CARTESIAN_POINT('Ctrl Pts',(17.4570587048633,-16.400088970387,1.82290968209227));
#212994=CARTESIAN_POINT('Ctrl Pts',(20.188569276403,-16.4969928998977,1.9500854887737));
#212995=CARTESIAN_POINT('Ctrl Pts',(21.58560319155,-18.8462140560325,2.07726129545514));
#212996=CARTESIAN_POINT('Ctrl Pts',(20.3664679748478,-21.2924869452229,
2.20443710213657));
#212997=CARTESIAN_POINT('Ctrl Pts',(17.6496448143142,-21.5915084873017,
2.33161290881801));
#212998=CARTESIAN_POINT('Ctrl Pts',(15.9276501817169,-19.4689447365969,
2.45878871549944));
#212999=CARTESIAN_POINT('Ctrl Pts',(16.7803073527985,-16.8721163178553,
2.58596452218088));
#213000=CARTESIAN_POINT('Ctrl Pts',(19.4253562537738,-16.1834520632443,
2.71314032886231));
#213001=CARTESIAN_POINT('Ctrl Pts',(21.4361287096228,-18.034758716609,2.84031613554374));
#213002=CARTESIAN_POINT('Ctrl Pts',(20.9678657836256,-20.72757731112,2.96749194222518));
#213003=CARTESIAN_POINT('Ctrl Pts',(18.4501696524655,-21.7914139305229,
3.09466774890661));
#213004=CARTESIAN_POINT('Ctrl Pts',(16.1928702476498,-20.2502645009728,
3.22184355558806));
#213005=CARTESIAN_POINT('Ctrl Pts',(16.2668996708449,-17.5180379719942,
3.34901936226947));
#213006=CARTESIAN_POINT('Ctrl Pts',(18.6043405202492,-16.1013826015585,
3.47619516895092));
#213007=CARTESIAN_POINT('Ctrl Pts',(21.0607358948925,-17.2999917651471,
3.60337097563235));
#213008=CARTESIAN_POINT('Ctrl Pts',(21.3824954994144,-20.0142159489022,
3.73054678231378));
#213009=CARTESIAN_POINT('Ctrl Pts',(19.2744248674316,-21.7539229281569,
3.85772258899522));
#213010=CARTESIAN_POINT('Ctrl Pts',(16.6705479621107,-20.9230395277464,
3.98489839567665));
#213011=CARTESIAN_POINT('Ctrl Pts',(15.9597602292861,-18.2838496971548,
4.11207420235809));
#213012=CARTESIAN_POINT('Ctrl Pts',(17.7941652973467,-16.2576462993305,
4.23925000903952));
#213013=CARTESIAN_POINT('Ctrl Pts',(20.4908103723742,-16.7033451914242,
4.36642581572096));
#213014=CARTESIAN_POINT('Ctrl Pts',(21.5756909706959,-19.2120453031261,
4.49360162240239));
#213015=CARTESIAN_POINT('Ctrl Pts',(20.053496478638,-21.4821699894429,4.62077742908383));
#213016=CARTESIAN_POINT('Ctrl Pts',(17.320745864617,-21.4310207505056,4.74795323576526));
#213017=CARTESIAN_POINT('Ctrl Pts',(15.8845682033658,-19.1055238383603,
4.8751290424467));
#213018=CARTESIAN_POINT('Ctrl Pts',(17.0625673598435,-16.6391783332833,
5.00230484912813));
#213019=CARTESIAN_POINT('Ctrl Pts',(19.7740022228553,-16.294703157517,5.12948065580956));
#213020=CARTESIAN_POINT('Ctrl Pts',(21.5312995962151,-18.388132904286,5.256656462491));
#213021=CARTESIAN_POINT('Ctrl Pts',(20.7222482100412,-20.9988757138337,
5.38383226917243));
#213022=CARTESIAN_POINT('Ctrl Pts',(18.0891024957557,-21.7317370993736,
5.51100807585386));
#213023=CARTESIAN_POINT('Ctrl Pts',(16.0476102147611,-19.9143622261804,
5.6381838825353));
#213024=CARTESIAN_POINT('Ctrl Pts',(16.4707138255686,-17.2140797414027,
5.76535968921673));
#213025=CARTESIAN_POINT('Ctrl Pts',(18.9702420260344,-16.1082312263917,
5.89253549589816));
#213026=CARTESIAN_POINT('Ctrl Pts',(21.2530328304472,-17.6113640569702,
6.01971130257961));
#213027=CARTESIAN_POINT('Ctrl Pts',(21.2247673617351,-20.3444471560277,
6.14688710926103));
#213028=CARTESIAN_POINT('Ctrl Pts',(18.9113774330884,-21.8000464144471,
6.27406291594248));
#213029=CARTESIAN_POINT('Ctrl Pts',(16.4352547188683,-20.6427398573077,
6.4012387226239));
#213030=CARTESIAN_POINT('Ctrl Pts',(16.0680881238634,-17.934284420239,6.52841452930535));
#213031=CARTESIAN_POINT('Ctrl Pts',(18.1467302100618,-16.1595198610482,
6.65559033598677));
#213032=CARTESIAN_POINT('Ctrl Pts',(20.7641558784545,-16.9466825084813,
6.78276614266821));
#213033=CARTESIAN_POINT('Ctrl Pts',(21.5190395340498,-19.5735994903424,
6.90994194934964));
#213034=CARTESIAN_POINT('Ctrl Pts',(19.7188222762027,-21.6302375206298,
7.03711775603107));
#213035=CARTESIAN_POINT('Ctrl Pts',(17.0150917049037,-21.2297588559072,
7.16429356271251));
#213036=CARTESIAN_POINT('Ctrl Pts',(15.8883528068746,-18.7395778145483,
7.29146936939395));
#213037=CARTESIAN_POINT('Ctrl Pts',(17.3723185877541,-16.4442809439337,
7.41864517607538));
#213038=CARTESIAN_POINT('Ctrl Pts',(20.1055425488892,-16.4496606606615,
7.54582098275682));
#213039=CARTESIAN_POINT('Ctrl Pts',(21.5804613489495,-18.7507814085371,
7.67299678943824));
#213040=CARTESIAN_POINT('Ctrl Pts',(20.4439285326649,-21.2365077250456,
7.80017259611969));
#213041=CARTESIAN_POINT('Ctrl Pts',(17.7386424177941,-21.6263399963654,
7.92734840280111));
#213042=CARTESIAN_POINT('Ctrl Pts',(15.9465351057383,-19.5626313092801,
8.05452420948256));
#213043=CARTESIAN_POINT('Ctrl Pts',(16.7117538245844,-16.9387062959837,
8.18170001616398));
#213044=CARTESIAN_POINT('Ctrl Pts',(19.3322578946213,-16.1618532970222,
8.30887582284543));
#213045=CARTESIAN_POINT('Ctrl Pts',(21.4038974784157,-17.9447867220078,
8.43605162952684));
#213046=CARTESIAN_POINT('Ctrl Pts',(21.0260718382901,-20.6517758148449,
8.5632274362083));
#213047=CARTESIAN_POINT('Ctrl Pts',(18.5454125485558,-21.799326097547,8.69040324288972));
#213048=CARTESIAN_POINT('Ctrl Pts',(16.2377705404641,-20.3346314107382,
8.81757904957116));
#213049=CARTESIAN_POINT('Ctrl Pts',(16.2202641280231,-17.6014582203607,
8.94475485625259));
#213050=CARTESIAN_POINT('Ctrl Pts',(18.5089543580768,-16.1073232887258,
9.07193066293403));
#213051=CARTESIAN_POINT('Ctrl Pts',(21.0041099966872,-17.223002679136,9.19910646961547));
#213052=CARTESIAN_POINT('Ctrl Pts',(21.4165806122538,-19.9249297977624,
9.32628227629688));
#213053=CARTESIAN_POINT('Ctrl Pts',(19.3679500158079,-21.7342542137755,
9.45345808297834));
#213054=CARTESIAN_POINT('Ctrl Pts',(16.7377096272338,-20.9910330748214,
9.58063388965975));
#213055=CARTESIAN_POINT('Ctrl Pts',(15.9389417519183,-18.3771256463843,
9.70780969634122));
#213056=CARTESIAN_POINT('Ctrl Pts',(17.7044663383378,-16.2906297566631,
9.83498550302262));
#213057=CARTESIAN_POINT('Ctrl Pts',(20.4145241592668,-16.6457758819371,
9.96216130970408));
#213058=CARTESIAN_POINT('Ctrl Pts',(21.5828053691612,-19.1167394951217,
10.0893371163855));
#213059=CARTESIAN_POINT('Ctrl Pts',(20.1374844696525,-21.4365648464185,
10.2165129230669));
#213060=CARTESIAN_POINT('Ctrl Pts',(17.4045536793081,-21.4769561606121,
10.3436887297484));
#213061=CARTESIAN_POINT('Ctrl Pts',(15.8913073734538,-19.2008569138979,
10.4708645364298));
#213062=CARTESIAN_POINT('Ctrl Pts',(16.9860551150528,-16.6964468944843,
10.5980403431112));
#213063=CARTESIAN_POINT('Ctrl Pts',(19.6844337988958,-16.2613668539671,
10.7252161497927));
#213064=CARTESIAN_POINT('Ctrl Pts',(21.5108484628264,-18.294775725408,10.8523919564741));
#213065=CARTESIAN_POINT('Ctrl Pts',(20.7896770127668,-20.9311470768482,
10.9795677631555));
#213066=CARTESIAN_POINT('Ctrl Pts',(18.1825494931985,-21.7517738250013,
11.106743569837));
#213067=CARTESIAN_POINT('Ctrl Pts',(16.081343586742,-20.0037818622775,11.2339193765184));
#213068=CARTESIAN_POINT('Ctrl Pts',(16.4137852970245,-17.2908453218587,
11.3610951831999));
#213069=CARTESIAN_POINT('Ctrl Pts',(18.8748799885214,-16.1019150957474,
11.4882709898813));
#213070=CARTESIAN_POINT('Ctrl Pts',(21.206726034548,-17.5277608730685,11.6154467965627));
#213071=CARTESIAN_POINT('Ctrl Pts',(21.2699994185634,-20.2602576510996,
11.7426226032442));
#213072=CARTESIAN_POINT('Ctrl Pts',(19.0066507379223,-21.7925092338742,
11.8697984099256));
#213073=CARTESIAN_POINT('Ctrl Pts',(16.4931619278508,-20.7187698964554,
11.996974216607));
#213074=CARTESIAN_POINT('Ctrl Pts',(16.0355029668799,-18.0241288371456,
12.1241500232885));
#213075=CARTESIAN_POINT('Ctrl Pts',(18.0535475461816,-16.1807519795754,
12.2513258299699));
#213076=CARTESIAN_POINT('Ctrl Pts',(20.6958650182194,-16.8798231776942,
12.3785016366513));
#213077=CARTESIAN_POINT('Ctrl Pts',(21.5382931031166,-19.4799879964801,
12.5056774433328));
#213078=CARTESIAN_POINT('Ctrl Pts',(19.8079563199639,-21.5957565991263,
12.6328532500142));
#213079=CARTESIAN_POINT('Ctrl Pts',(17.092331270491,-21.2860426121147,12.7600290566956));
#213080=CARTESIAN_POINT('Ctrl Pts',(15.8828353868898,-18.8349893955103,
12.8872048633771));
#213081=CARTESIAN_POINT('Ctrl Pts',(17.2891060725835,-16.491286146028,13.0143806700585));
#213082=CARTESIAN_POINT('Ctrl Pts',(20.0209772564507,-16.4051351284387,
13.1415564767399));
#213083=CARTESIAN_POINT('Ctrl Pts',(21.5721266863414,-18.6555745542452,
13.2687322834214));
#213084=CARTESIAN_POINT('Ctrl Pts',(20.5194710355226,-21.1779659282937,
13.3959080901028));
#213085=CARTESIAN_POINT('Ctrl Pts',(17.8287565284422,-21.6581717221597,
13.5230838967842));
#213086=CARTESIAN_POINT('Ctrl Pts',(15.9685467207697,-19.6556329249039,
13.6502597034657));
#213087=CARTESIAN_POINT('Ctrl Pts',(16.6454686534027,-17.0075545914336,
13.7774355101471));
#213088=CARTESIAN_POINT('Ctrl Pts',(19.2384884676639,-16.14338423443,13.9046113168286));
#213089=CARTESIAN_POINT('Ctrl Pts',(21.3686714249291,-17.8559445199825,
14.03178712351));
#213090=CARTESIAN_POINT('Ctrl Pts',(21.0817068759728,-20.5740676795759,
14.1589629301914));
#213091=CARTESIAN_POINT('Ctrl Pts',(18.6408669834337,-21.8040444200327,
14.2861387368729));
#213092=CARTESIAN_POINT('Ctrl Pts',(16.2854708531072,-20.4174474229502,
14.4133145435543));
#213093=CARTESIAN_POINT('Ctrl Pts',(16.1764482421967,-17.6863933712359,
14.5404903502357));
#213094=CARTESIAN_POINT('Ctrl Pts',(18.413820629506,-16.1164548490061,14.6676661569172));
#213095=CARTESIAN_POINT('Ctrl Pts',(20.9449377166707,-17.1479530090328,
14.7948419635986));
#213096=CARTESIAN_POINT('Ctrl Pts',(21.4476566750608,-19.8345523114875,
14.92201777028));
#213097=CARTESIAN_POINT('Ctrl Pts',(19.4607640626112,-21.7114646455266,
15.0491935769614));
#213098=CARTESIAN_POINT('Ctrl Pts',(16.8071105307807,-21.0567394389867,
15.1763693836429));
#213099=CARTESIAN_POINT('Ctrl Pts',(15.9212584907105,-18.471046432039,15.3035451903243));
#213100=CARTESIAN_POINT('Ctrl Pts',(17.6159222069866,-16.3265984723504,
15.4307209970058));
#213101=CARTESIAN_POINT('Ctrl Pts',(20.3363529026182,-16.5907934634841,
15.5578968036872));
#213102=CARTESIAN_POINT('Ctrl Pts',(21.5867242633349,-19.0212488988654,
15.6850726103686));
#213103=CARTESIAN_POINT('Ctrl Pts',(20.2198981724784,-21.388172767609,15.8122484170501));
#213104=CARTESIAN_POINT('Ctrl Pts',(17.4898527336144,-21.5200593280063,
15.9394242237315));
#213105=CARTESIAN_POINT('Ctrl Pts',(15.9012351911711,-19.2959108466956,
16.0666000304129));
#213106=CARTESIAN_POINT('Ctrl Pts',(16.9115035396152,-16.7562455090563,
16.1937758370943));
#213107=CARTESIAN_POINT('Ctrl Pts',(19.5937992735749,-16.2310486329641,
16.3209516437758));
#213108=CARTESIAN_POINT('Ctrl Pts',(21.4872825391909,-18.2021557548393,
16.4481274504572));
#213109=CARTESIAN_POINT('Ctrl Pts',(20.8547999630863,-20.8611984310668,
16.5753032571387));
#213110=CARTESIAN_POINT('Ctrl Pts',(18.2766150525408,-21.7686700450093,
16.7024790638201));
#213111=CARTESIAN_POINT('Ctrl Pts',(16.1180524427778,-20.092021714915,16.8296548705015));
#213112=CARTESIAN_POINT('Ctrl Pts',(16.3594593527494,-17.3694742191139,
16.956830677183));
#213113=CARTESIAN_POINT('Ctrl Pts',(18.7793599259594,-16.0987959046484,
17.0840064838644));
#213114=CARTESIAN_POINT('Ctrl Pts',(21.1576455824562,-17.4457552578498,
17.2111822905458));
#213115=CARTESIAN_POINT('Ctrl Pts',(21.3123868454594,-20.1746006738818,
17.3383580972273));
#213116=CARTESIAN_POINT('Ctrl Pts',(19.1016182104896,-21.7817858547834,
17.4655339039087));
#213117=CARTESIAN_POINT('Ctrl Pts',(16.5535826843549,-20.7928181502387,
17.5927097105901));
#213118=CARTESIAN_POINT('Ctrl Pts',(16.0059447133635,-18.1150140469113,
17.7198855172716));
#213119=CARTESIAN_POINT('Ctrl Pts',(17.9611281456538,-16.2050926063331,
17.847061323953));
#213120=CARTESIAN_POINT('Ctrl Pts',(20.6253735344697,-16.8152882071486,
17.9742371306345));
#213121=CARTESIAN_POINT('Ctrl Pts',(21.55440109729,-19.3857842586047,18.1014129373159));
#213122=CARTESIAN_POINT('Ctrl Pts',(19.8958857071821,-21.5583101764979,
18.2285887439973));
#213123=CARTESIAN_POINT('Ctrl Pts',(17.171412295493,-21.3397082732704,18.3557645506787));
#213124=CARTESIAN_POINT('Ctrl Pts',(15.8805161175613,-18.9305322272779,
18.4829403573602));
#213125=CARTESIAN_POINT('Ctrl Pts',(17.2075142945774,-16.54105153018,18.6101161640416));
#213126=CARTESIAN_POINT('Ctrl Pts',(19.9349683619421,-16.3634664140689,
18.7372919707231));
#213127=CARTESIAN_POINT('Ctrl Pts',(21.5606084977061,-18.5607002000248,
18.8644677774045));
#213128=CARTESIAN_POINT('Ctrl Pts',(20.5930107759761,-21.1169272666383,
18.9916435840859));
#213129=CARTESIAN_POINT('Ctrl Pts',(17.9198860504282,-21.6869679347534,
19.1188193907673));
#213130=CARTESIAN_POINT('Ctrl Pts',(15.9936603441588,-19.7478452776443,
19.2459951974488));
#213131=CARTESIAN_POINT('Ctrl Pts',(16.5815261871606,-17.078583966977,19.3731710041302));
#213132=CARTESIAN_POINT('Ctrl Pts',(19.1441531564327,-16.1280656028778,
19.5003468108116));
#213133=CARTESIAN_POINT('Ctrl Pts',(21.3304900605322,-17.768331748829,19.6275226174931));
#213134=CARTESIAN_POINT('Ctrl Pts',(21.1347084926027,-20.4945400989296,
19.7546984241745));
#213135=CARTESIAN_POINT('Ctrl Pts',(18.7364258833193,-21.8055635519036,
19.881874230856));
#213136=CARTESIAN_POINT('Ctrl Pts',(16.335917684683,-20.4986197454331,20.0090500375374));
#213137=CARTESIAN_POINT('Ctrl Pts',(16.13550115311,-17.7727479556429,20.1362258442188));
#213138=CARTESIAN_POINT('Ctrl Pts',(18.3190460623333,-16.1287674194462,
20.2634016509003));
#213139=CARTESIAN_POINT('Ctrl Pts',(20.8832853969895,-17.0749262060105,
20.3905774575817));
#213140=CARTESIAN_POINT('Ctrl Pts',(21.4756888902747,-19.7431862770776,
20.5177532642631));
#213141=CARTESIAN_POINT('Ctrl Pts',(19.5527627818701,-21.6855770682093,
20.6449290709446));
#213142=CARTESIAN_POINT('Ctrl Pts',(16.8786730502231,-21.1200901556103,
20.772104877626));
#213143=CARTESIAN_POINT('Ctrl Pts',(15.9067298484541,-18.5654966090028,
20.8992806843074));
#213144=CARTESIAN_POINT('Ctrl Pts',(17.5286330567039,-16.3655315522399,
21.0264564909889));
#213145=CARTESIAN_POINT('Ctrl Pts',(20.256382680945,-16.5384221250544,21.1536322976703));
#213146=CARTESIAN_POINT('Ctrl Pts',(21.5874463526494,-18.9257528612692,
21.2808081043517));
#213147=CARTESIAN_POINT('Ctrl Pts',(20.3006391779602,-21.3369088308205,
21.4079839110332));
#213148=CARTESIAN_POINT('Ctrl Pts',(17.5765588536269,-21.5605501870015,
21.5351597177146));
#213149=CARTESIAN_POINT('Ctrl Pts',(15.9143182549829,-19.3900617201843,
21.6623355243961));
#213150=CARTESIAN_POINT('Ctrl Pts',(16.8390400444023,-16.8195068044844,
21.7895113310775));
#213151=CARTESIAN_POINT('Ctrl Pts',(19.5021076033005,-16.2018289998698,
21.9166871377589));
#213152=CARTESIAN_POINT('Ctrl Pts',(21.4611728203329,-18.1146776111084,
22.0438816020413));
#213153=CARTESIAN_POINT('Ctrl Pts',(21.0977299961801,-19.8915948627883,
22.1286841307634));
#213154=CARTESIAN_POINT('Ctrl Pts',(20.5799309501441,-20.506446466246,22.171094723925));
#213155=CARTESIAN_POINT('Ctrl Pts',(18.1489776385292,-21.138301703768,-0.171345817110153));
#213156=CARTESIAN_POINT('Ctrl Pts',(17.4210583610835,-20.9435211508747,
-0.128953881549675));
#213157=CARTESIAN_POINT('Ctrl Pts',(16.1877699881095,-19.77288952068,-0.0441700104287193));
#213158=CARTESIAN_POINT('Ctrl Pts',(16.6662106246443,-17.2504067355124,
0.0830057962527148));
#213159=CARTESIAN_POINT('Ctrl Pts',(19.0452436391262,-16.2947305011482,
0.210181602934149));
#213160=CARTESIAN_POINT('Ctrl Pts',(21.1369461776993,-17.7741154785761,
0.337357409615584));
#213161=CARTESIAN_POINT('Ctrl Pts',(21.0250156451928,-20.3355843150782,
0.464533216297019));
#213162=CARTESIAN_POINT('Ctrl Pts',(18.8107430711202,-21.6269506071525,
0.591709022978452));
#213163=CARTESIAN_POINT('Ctrl Pts',(16.5263111681857,-20.4646046776889,
0.718884829659889));
#213164=CARTESIAN_POINT('Ctrl Pts',(16.2671682231216,-17.9143360270367,
0.84606063634132));
#213165=CARTESIAN_POINT('Ctrl Pts',(18.2712570171198,-16.3161643914318,
0.973236443022757));
#213166=CARTESIAN_POINT('Ctrl Pts',(20.6998491681173,-17.1361539837924,
1.10041224970419));
#213167=CARTESIAN_POINT('Ctrl Pts',(21.3249146812175,-19.6220977928601,
1.22758805638563));
#213168=CARTESIAN_POINT('Ctrl Pts',(19.5729674648886,-21.4932538336279,
1.35476386306706));
#213169=CARTESIAN_POINT('Ctrl Pts',(17.0513245079943,-21.0329748042223,
1.4819396697485));
#213170=CARTESIAN_POINT('Ctrl Pts',(16.0734293667079,-18.6635266109603,
1.60911547642993));
#213171=CARTESIAN_POINT('Ctrl Pts',(17.5364439501815,-16.5587368924863,
1.73629128311137));
#213172=CARTESIAN_POINT('Ctrl Pts',(20.0981412048233,-16.6496164712725,
1.8634670897928));
#213173=CARTESIAN_POINT('Ctrl Pts',(21.4083239228994,-18.852790586328,1.99064289647423));
#213174=CARTESIAN_POINT('Ctrl Pts',(20.264980246985,-21.1469828950223,2.11781870315567));
#213175=CARTESIAN_POINT('Ctrl Pts',(17.717057312254,-21.4274147818336,2.2449945098371));
#213176=CARTESIAN_POINT('Ctrl Pts',(16.1021161259398,-19.4368071709258,
2.37217031651854));
#213177=CARTESIAN_POINT('Ctrl Pts',(16.9017650663717,-17.0014191111546,
2.49934612319997));
#213178=CARTESIAN_POINT('Ctrl Pts',(19.3823758238848,-16.3555679294722,
2.62652192988141));
#213179=CARTESIAN_POINT('Ctrl Pts',(21.2681420125742,-18.0917820305039,
2.75369773656284));
#213180=CARTESIAN_POINT('Ctrl Pts',(20.8289901877649,-20.6171927218193,
2.88087354324428));
#213181=CARTESIAN_POINT('Ctrl Pts',(18.467814897281,-21.6148924472776,3.0080493499257));
#213182=CARTESIAN_POINT('Ctrl Pts',(16.3508479162741,-20.1695536286012,
3.13522515660715));
#213183=CARTESIAN_POINT('Ctrl Pts',(16.4202750574822,-17.6071849263638,
3.26240096328857));
#213184=CARTESIAN_POINT('Ctrl Pts',(18.612401227227,-16.278600585146,3.38957676997001));
#213185=CARTESIAN_POINT('Ctrl Pts',(20.9160867238537,-17.4026942773856,
3.51675257665145));
#213186=CARTESIAN_POINT('Ctrl Pts',(21.2178430868515,-19.9481798092568,
3.64392838333288));
#213187=CARTESIAN_POINT('Ctrl Pts',(19.2408275823876,-21.5797321960836,
3.77110419001432));
#213188=CARTESIAN_POINT('Ctrl Pts',(16.7988292283319,-20.8005033884281,
3.89827999669575));
#213189=CARTESIAN_POINT('Ctrl Pts',(16.1322299470473,-18.3253874529646,
4.02545580337718));
#213190=CARTESIAN_POINT('Ctrl Pts',(17.8525932052803,-16.4251496374373,
4.15263161005862));
#213191=CARTESIAN_POINT('Ctrl Pts',(20.3815924913958,-16.8431401955444,
4.27980741674006));
#213192=CARTESIAN_POINT('Ctrl Pts',(21.3990279277772,-19.1958787336361,
4.40698322342148));
#213193=CARTESIAN_POINT('Ctrl Pts',(19.9714656507117,-21.3248736704392,
4.53415903010293));
#213194=CARTESIAN_POINT('Ctrl Pts',(17.4086054448983,-21.2769042917635,
4.66133483678435));
#213195=CARTESIAN_POINT('Ctrl Pts',(16.0617124801271,-19.0959795252294,
4.78851064346579));
#213196=CARTESIAN_POINT('Ctrl Pts',(17.1664774539701,-16.7829624806744,
4.91568645014722));
#213197=CARTESIAN_POINT('Ctrl Pts',(19.709347072374,-16.4599027344493,5.04286225682866));
#213198=CARTESIAN_POINT('Ctrl Pts',(21.3573962887413,-18.4231875523662,
5.1700380635101));
#213199=CARTESIAN_POINT('Ctrl Pts',(20.5986422365255,-20.8716249691852,
5.29721387019152));
#213200=CARTESIAN_POINT('Ctrl Pts',(18.1291946650469,-21.5589256221392,
5.42438967687296));
#213201=CARTESIAN_POINT('Ctrl Pts',(16.2146184499352,-19.8545338208328,
5.55156548355439));
#213202=CARTESIAN_POINT('Ctrl Pts',(16.6114184365535,-17.3221232564787,
5.67874129023583));
#213203=CARTESIAN_POINT('Ctrl Pts',(18.9555552653643,-16.2850234427458,
5.80591709691726));
#213204=CARTESIAN_POINT('Ctrl Pts',(21.096428889474,-17.69470908906,5.9330929035987));
#213205=CARTESIAN_POINT('Ctrl Pts',(21.0699206363647,-20.2578811098868,
6.06026871028013));
#213206=CARTESIAN_POINT('Ctrl Pts',(18.9003501829765,-21.6229882645151,
6.18744451696157));
#213207=CARTESIAN_POINT('Ctrl Pts',(16.5781637615641,-20.537629466679,6.31462032364299));
#213208=CARTESIAN_POINT('Ctrl Pts',(16.2338232826291,-17.9975540484287,
6.44179613032444));
#213209=CARTESIAN_POINT('Ctrl Pts',(18.1832397634138,-16.3331235511484,
6.56897193700587));
#213210=CARTESIAN_POINT('Ctrl Pts',(20.6379445772308,-17.0713496498852,
6.69614774368731));
#213211=CARTESIAN_POINT('Ctrl Pts',(21.3458984135663,-19.5349557185273,
6.82332355036874));
#213212=CARTESIAN_POINT('Ctrl Pts',(19.6575975681531,-21.4637360977331,
6.95049935705017));
#213213=CARTESIAN_POINT('Ctrl Pts',(17.1219532788895,-21.0881545031928,
7.07767516373161));
#213214=CARTESIAN_POINT('Ctrl Pts',(16.0652618013412,-18.7527837366743,
7.20485097041304));
#213215=CARTESIAN_POINT('Ctrl Pts',(17.4569719804889,-16.6001815270014,
7.33202677709449));
#213216=CARTESIAN_POINT('Ctrl Pts',(20.0202761062402,-16.6052267959878,
7.4592025837759));
#213217=CARTESIAN_POINT('Ctrl Pts',(21.4035017398149,-18.7632908224833,
7.58637839045736));
#213218=CARTESIAN_POINT('Ctrl Pts',(20.3376252150735,-21.094483806738,7.71355419713877));
#213219=CARTESIAN_POINT('Ctrl Pts',(17.8005220877082,-21.4600808758526,
7.84073000382022));
#213220=CARTESIAN_POINT('Ctrl Pts',(16.1198270066971,-19.5246694104279,
7.96790581050164));
#213221=CARTESIAN_POINT('Ctrl Pts',(16.8374733931665,-17.0638693048078,
8.09508161718309));
#213222=CARTESIAN_POINT('Ctrl Pts',(19.295065229689,-16.335311921419,8.22225742386451));
#213223=CARTESIAN_POINT('Ctrl Pts',(21.2379145416073,-18.0074034401497,
8.34943323054596));
#213224=CARTESIAN_POINT('Ctrl Pts',(20.8835776720644,-20.5461036742685,
8.47660903722738));
#213225=CARTESIAN_POINT('Ctrl Pts',(18.5571367062394,-21.6223127284784,
8.60378484390882));
#213226=CARTESIAN_POINT('Ctrl Pts',(16.3929568350657,-20.2486755926092,
8.73096065059025));
#213227=CARTESIAN_POINT('Ctrl Pts',(16.3765387661935,-17.6854190812848,
8.85813645727169));
#213228=CARTESIAN_POINT('Ctrl Pts',(18.5229450587927,-16.2841719500039,
8.98531226395313));
#213229=CARTESIAN_POINT('Ctrl Pts',(20.8629811604026,-17.3304914705113,
9.11248807063455));
#213230=CARTESIAN_POINT('Ctrl Pts',(21.2498091868164,-19.8644444246549,
9.23966387731599));
#213231=CARTESIAN_POINT('Ctrl Pts',(19.3285384330547,-21.5612862518657,
9.36683968399743));
#213232=CARTESIAN_POINT('Ctrl Pts',(16.861815568182,-20.864269893559,9.49401549067886));
#213233=CARTESIAN_POINT('Ctrl Pts',(16.1127057186315,-18.4128645967674,
9.6211912973603));
#213234=CARTESIAN_POINT('Ctrl Pts',(17.7684706763648,-16.4560825699245,
9.74836710404172));
#213235=CARTESIAN_POINT('Ctrl Pts',(20.310048861025,-16.7891498710692,9.87554291072316));
#213236=CARTESIAN_POINT('Ctrl Pts',(21.4057000363191,-19.1064979238893,
10.0027187174046));
#213237=CARTESIAN_POINT('Ctrl Pts',(20.0502322526962,-21.2821037207635,
10.129894524086));
#213238=CARTESIAN_POINT('Ctrl Pts',(17.4872030718116,-21.3199839763846,
10.2570703307675));
#213239=CARTESIAN_POINT('Ctrl Pts',(16.068032687595,-19.1853859073339,10.3842461374489));
#213240=CARTESIAN_POINT('Ctrl Pts',(17.0947218439171,-16.8366707538674,
10.5114219441303));
#213241=CARTESIAN_POINT('Ctrl Pts',(19.6253469633683,-16.4286388915877,
10.6385977508117));
#213242=CARTESIAN_POINT('Ctrl Pts',(21.3382165671608,-18.3356342288226,
10.7657735574932));
#213243=CARTESIAN_POINT('Ctrl Pts',(20.6618791064926,-20.8081069051386,
10.8929493641746));
#213244=CARTESIAN_POINT('Ctrl Pts',(18.2168322232895,-21.577716698977,11.0201251708561));
#213245=CARTESIAN_POINT('Ctrl Pts',(16.2462546761661,-19.9383943918618,
11.1473009775375));
#213246=CARTESIAN_POINT('Ctrl Pts',(16.5580290567716,-17.3941164527542,
11.2744767842189));
#213247=CARTESIAN_POINT('Ctrl Pts',(18.8661217218008,-16.2790999750865,
11.4016525909004));
#213248=CARTESIAN_POINT('Ctrl Pts',(21.0530009074768,-17.6163033713916,
11.5288283975818));
#213249=CARTESIAN_POINT('Ctrl Pts',(21.1123406939717,-20.1789255217625,
11.6560042042632));
#213250=CARTESIAN_POINT('Ctrl Pts',(18.989700510219,-21.6159196575024,11.7831800109447));
#213251=CARTESIAN_POINT('Ctrl Pts',(16.6324709789039,-20.6089328489849,
11.9103558176261));
#213252=CARTESIAN_POINT('Ctrl Pts',(16.203263888843,-18.0818129923747,12.0375316243075));
#213253=CARTESIAN_POINT('Ctrl Pts',(18.0958501055707,-16.3530357053638,
12.164707430989));
#213254=CARTESIAN_POINT('Ctrl Pts',(20.5738992423879,-17.0086468487652,
12.2918832376704));
#213255=CARTESIAN_POINT('Ctrl Pts',(21.3639550213402,-19.4471638903247,
12.4190590443519));
#213256=CARTESIAN_POINT('Ctrl Pts',(19.7411903016307,-21.4313987958485,
12.5462348510332));
#213257=CARTESIAN_POINT('Ctrl Pts',(17.1943909934554,-21.140939195026,12.6734106577147));
#213258=CARTESIAN_POINT('Ctrl Pts',(16.0600873898727,-18.8422637436558,
12.8005864643961));
#213259=CARTESIAN_POINT('Ctrl Pts',(17.3789326443482,-16.6442644964813,
12.9277622710776));
#213260=CARTESIAN_POINT('Ctrl Pts',(19.9409680926688,-16.563469339566,13.054938077759));
#213261=CARTESIAN_POINT('Ctrl Pts',(21.3956852288542,-18.6740028146668,
13.1821138844404));
#213262=CARTESIAN_POINT('Ctrl Pts',(20.4084713703825,-21.0395814528595,
13.3092896911219));
#213263=CARTESIAN_POINT('Ctrl Pts',(17.8850339589992,-21.4899336779714,
13.4364654978033));
#213264=CARTESIAN_POINT('Ctrl Pts',(16.1404701974589,-19.6118892754737,
13.5636413044848));
#213265=CARTESIAN_POINT('Ctrl Pts',(16.7753090571362,-17.1284374200765,
13.6908171111662));
#213266=CARTESIAN_POINT('Ctrl Pts',(19.2071252868205,-16.3179910487006,
13.8179929178476));
#213267=CARTESIAN_POINT('Ctrl Pts',(21.2048784313142,-17.9240844051089,
13.945168724529));
#213268=CARTESIAN_POINT('Ctrl Pts',(20.9357539750881,-20.4732265201925,
14.0723445312105));
#213269=CARTESIAN_POINT('Ctrl Pts',(18.6466569029825,-21.6267377209658,
14.1995203378919));
#213270=CARTESIAN_POINT('Ctrl Pts',(16.4376917012663,-20.3263430756987,
14.3266961445733));
#213271=CARTESIAN_POINT('Ctrl Pts',(16.3354468386715,-17.7650739598295,
14.4538719512548));
#213272=CARTESIAN_POINT('Ctrl Pts',(18.4337256305968,-16.2927358168784,
14.5810477579362));
#213273=CARTESIAN_POINT('Ctrl Pts',(20.8074875193202,-17.2601075093917,
14.7082235646177));
#213274=CARTESIAN_POINT('Ctrl Pts',(21.2789533042171,-19.7796855513471,
14.8353993712991));
#213275=CARTESIAN_POINT('Ctrl Pts',(19.4155823901109,-21.5399134719006,
14.9625751779805));
#213276=CARTESIAN_POINT('Ctrl Pts',(16.9269019368522,-20.9258914060103,
15.089750984662));
#213277=CARTESIAN_POINT('Ctrl Pts',(16.0961217953763,-18.5009464886232,
15.2169267913434));
#213278=CARTESIAN_POINT('Ctrl Pts',(17.6854311814566,-16.489815172386,15.3441025980248));
#213279=CARTESIAN_POINT('Ctrl Pts',(20.2367373770296,-16.7375856150594,
15.4712784047062));
#213280=CARTESIAN_POINT('Ctrl Pts',(21.4093752995786,-19.0169438138584,
15.5984542113877));
#213281=CARTESIAN_POINT('Ctrl Pts',(20.1275224372825,-21.2367200943101,
15.7256300180691));
#213282=CARTESIAN_POINT('Ctrl Pts',(17.5671992305365,-21.3604074939539,
15.8528058247506));
#213283=CARTESIAN_POINT('Ctrl Pts',(16.0773433099501,-19.2745305005226,
15.979981631432));
#213284=CARTESIAN_POINT('Ctrl Pts',(17.0248050117741,-16.8927517913624,
16.1071574381134));
#213285=CARTESIAN_POINT('Ctrl Pts',(19.5403470306901,-16.4002055022689,
16.2343332447949));
#213286=CARTESIAN_POINT('Ctrl Pts',(21.3161156964891,-18.2487722826149,
16.3615090514763));
#213287=CARTESIAN_POINT('Ctrl Pts',(20.7229534749337,-20.7425068464271,
16.4886848581577));
#213288=CARTESIAN_POINT('Ctrl Pts',(18.3050498885018,-21.5935625100306,
16.6158606648392));
#213289=CARTESIAN_POINT('Ctrl Pts',(16.2806814057228,-20.021148524541,16.7430364715206));
#213290=CARTESIAN_POINT('Ctrl Pts',(16.5070804630683,-17.4678571266262,
16.870212278202));
#213291=CARTESIAN_POINT('Ctrl Pts',(18.776539977334,-16.2761746987364,16.9973880848835));
#213292=CARTESIAN_POINT('Ctrl Pts',(21.0069717027245,-17.5393959043074,
17.1245638915649));
#213293=CARTESIAN_POINT('Ctrl Pts',(21.1520929673995,-20.0985936915781,
17.2517396982463));
#213294=CARTESIAN_POINT('Ctrl Pts',(19.0787640182614,-21.6058629324566,
17.3789155049278));
#213295=CARTESIAN_POINT('Ctrl Pts',(16.6891354808367,-20.6783776501158,
17.5060913116092));
#213296=CARTESIAN_POINT('Ctrl Pts',(16.1755432211384,-18.1670480248764,
17.6332671182907));
#213297=CARTESIAN_POINT('Ctrl Pts',(18.0091762603091,-16.3758631171963,
17.760442924972));
#213298=CARTESIAN_POINT('Ctrl Pts',(20.5077900930114,-16.9481239064058,
17.8876187316535));
#213299=CARTESIAN_POINT('Ctrl Pts',(21.3790616092047,-19.3588166369015,
18.0147945383349));
#213300=CARTESIAN_POINT('Ctrl Pts',(19.8236532699919,-21.3962803529462,
18.1419703450164));
#213301=CARTESIAN_POINT('Ctrl Pts',(17.2685556870694,-21.1912685542763,
18.2691461516978));
#213302=CARTESIAN_POINT('Ctrl Pts',(16.0579123055315,-18.931866841806,18.3963219583793));
#213303=CARTESIAN_POINT('Ctrl Pts',(17.3024132869284,-16.6909360522447,
18.5234977650607));
#213304=CARTESIAN_POINT('Ctrl Pts',(19.8603062232868,-16.5243910975421,
18.6506735717421));
#213305=CARTESIAN_POINT('Ctrl Pts',(21.3848831062071,-18.5850266359637,
18.7778493784235));
#213306=CARTESIAN_POINT('Ctrl Pts',(20.4774392715833,-20.9823374598767,
18.905025185105));
#213307=CARTESIAN_POINT('Ctrl Pts',(17.9704981152505,-21.5169396795275,
19.0322009917864));
#213308=CARTESIAN_POINT('Ctrl Pts',(16.164022550051,-19.6983689447528,19.1593767984678));
#213309=CARTESIAN_POINT('Ctrl Pts',(16.7153417841063,-17.1950510214384,
19.2865526051493));
#213310=CARTESIAN_POINT('Ctrl Pts',(19.1186546397307,-16.3036247501402,
19.4137284118307));
#213311=CARTESIAN_POINT('Ctrl Pts',(21.1690707367099,-17.8419183693358,
19.5409042185122));
#213312=CARTESIAN_POINT('Ctrl Pts',(20.9854605723195,-20.3986430325311,
19.6680800251936));
#213313=CARTESIAN_POINT('Ctrl Pts',(18.7362750703233,-21.6281624110196,
19.795255831875));
#213314=CARTESIAN_POINT('Ctrl Pts',(16.4850023400387,-20.4024690544242,
19.9224316385565));
#213315=CARTESIAN_POINT('Ctrl Pts',(16.2970453597273,-17.8460600281632,
20.0496074452379));
#213316=CARTESIAN_POINT('Ctrl Pts',(18.3448430353522,-16.3042829359788,
20.1767832519193));
#213317=CARTESIAN_POINT('Ctrl Pts',(20.7496680183763,-17.1916206571837,
20.3039590586007));
#213318=CARTESIAN_POINT('Ctrl Pts',(21.305242804797,-19.6939995862426,20.4311348652822));
#213319=CARTESIAN_POINT('Ctrl Pts',(19.5018617071349,-21.5156352807656,
20.5583106719636));
#213320=CARTESIAN_POINT('Ctrl Pts',(16.9940155374735,-20.9853037174782,
20.6854864786451));
#213321=CARTESIAN_POINT('Ctrl Pts',(16.082496373835,-18.5895248604405,20.8126622853265));
#213322=CARTESIAN_POINT('Ctrl Pts',(17.6035686476012,-16.5263278496229,
20.9398380920079));
#213323=CARTESIAN_POINT('Ctrl Pts',(20.1617387665729,-16.6884701127161,
21.0670138986894));
#213324=CARTESIAN_POINT('Ctrl Pts',(21.4100524978415,-18.9273846007665,
21.1941897053708));
#213325=CARTESIAN_POINT('Ctrl Pts',(20.2032439132434,-21.1886431483515,
21.3213655120522));
#213326=CARTESIAN_POINT('Ctrl Pts',(17.6485149801115,-21.3983811058473,
21.4485413187337));
#213327=CARTESIAN_POINT('Ctrl Pts',(16.0896130221739,-19.3628281760474,
21.5757171254151));
#213328=CARTESIAN_POINT('Ctrl Pts',(16.9568464474972,-16.9520802407969,
21.7028929320966));
#213329=CARTESIAN_POINT('Ctrl Pts',(19.4543556739431,-16.3728024035369,
21.8300687387779));
#213330=CARTESIAN_POINT('Ctrl Pts',(21.291629173971,-18.1667325047092,21.9572632030605));
#213331=CARTESIAN_POINT('Ctrl Pts',(20.9507809654552,-19.8331818652868,
22.0420657317825));
#213332=CARTESIAN_POINT('Ctrl Pts',(20.4651725960397,-20.4098092014579,
22.084476324944));
#213333=CARTESIAN_POINT('Ctrl Pts',(18.187758406819,-20.9933731243335,-0.257964216091064));
#213334=CARTESIAN_POINT('Ctrl Pts',(17.5080924453001,-20.811504453082,-0.215572280530586));
#213335=CARTESIAN_POINT('Ctrl Pts',(16.3565579911106,-19.7184732651834,
-0.13078840940963));
#213336=CARTESIAN_POINT('Ctrl Pts',(16.8032830955771,-17.3632042941351,
-0.00361260272819575));
#213337=CARTESIAN_POINT('Ctrl Pts',(19.0246114919716,-16.4708792426415,
0.123563203953239));
#213338=CARTESIAN_POINT('Ctrl Pts',(20.977656370903,-17.8521967105184,0.250739010634673));
#213339=CARTESIAN_POINT('Ctrl Pts',(20.8731456437434,-20.2438673718189,
0.377914817316107));
#213340=CARTESIAN_POINT('Ctrl Pts',(18.805655820692,-21.4496297959928,0.505090623997542));
#213341=CARTESIAN_POINT('Ctrl Pts',(16.6726574870295,-20.3643350548799,
0.632266430678976));
#213342=CARTESIAN_POINT('Ctrl Pts',(16.4306929665323,-17.9831221260791,
0.75944223736041));
#213343=CARTESIAN_POINT('Ctrl Pts',(18.3019319614957,-16.490892293676,0.886618044041845));
#213344=CARTESIAN_POINT('Ctrl Pts',(20.5695342500862,-17.2565252862285,
1.01379385072328));
#213345=CARTESIAN_POINT('Ctrl Pts',(21.1531645592934,-19.5776774271649,
1.14096965740471));
#213346=CARTESIAN_POINT('Ctrl Pts',(19.5173528337202,-21.3247956983873,
1.26814546408615));
#213347=CARTESIAN_POINT('Ctrl Pts',(17.1628680192514,-20.8950282794151,
1.39532127076758));
#213348=CARTESIAN_POINT('Ctrl Pts',(16.249796938349,-18.6826493324063,1.52249707744901));
#213349=CARTESIAN_POINT('Ctrl Pts',(17.6158291954999,-16.7173848145856,
1.64967288413045));
#213350=CARTESIAN_POINT('Ctrl Pts',(20.0077131332437,-16.8022400426472,
1.77684869081188));
#213351=CARTESIAN_POINT('Ctrl Pts',(21.2310446542488,-18.8593671166236,
1.90402449749332));
#213352=CARTESIAN_POINT('Ctrl Pts',(20.1634925191223,-21.0014788448218,
2.03120030417475));
#213353=CARTESIAN_POINT('Ctrl Pts',(17.7844698101939,-21.2633210763656,
2.15837611085619));
#213354=CARTESIAN_POINT('Ctrl Pts',(16.2765820701628,-19.4046696052545,
2.28555191753762));
#213355=CARTESIAN_POINT('Ctrl Pts',(17.0232227799449,-17.1307219044541,
2.41272772421906));
#213356=CARTESIAN_POINT('Ctrl Pts',(19.3393953939956,-16.5276837957002,
2.53990353090049));
#213357=CARTESIAN_POINT('Ctrl Pts',(21.1001553155256,-18.148805344399,2.66707933758192));
#213358=CARTESIAN_POINT('Ctrl Pts',(20.6901145919042,-20.5068081325184,
2.79425514426337));
#213359=CARTESIAN_POINT('Ctrl Pts',(18.4854601420967,-21.4383709640324,
2.92143095094479));
#213360=CARTESIAN_POINT('Ctrl Pts',(16.5088255848986,-20.0888427562296,
3.04860675762623));
#213361=CARTESIAN_POINT('Ctrl Pts',(16.5736504441196,-17.6963318807336,
3.17578256430766));
#213362=CARTESIAN_POINT('Ctrl Pts',(18.6204619342047,-16.4558185687336,
3.3029583709891));
#213363=CARTESIAN_POINT('Ctrl Pts',(20.7714375528147,-17.5053967896241,
3.43013417767053));
#213364=CARTESIAN_POINT('Ctrl Pts',(21.0531906742887,-19.8821436696115,
3.55730998435197));
#213365=CARTESIAN_POINT('Ctrl Pts',(19.2072302973436,-21.4055414640101,
3.6844857910334));
#213366=CARTESIAN_POINT('Ctrl Pts',(16.9271104945531,-20.6779672491097,
3.81166159771483));
#213367=CARTESIAN_POINT('Ctrl Pts',(16.3046996648085,-18.3669252087745,
3.93883740439627));
#213368=CARTESIAN_POINT('Ctrl Pts',(17.9110211132137,-16.5926529755442,
4.0660132110777));
#213369=CARTESIAN_POINT('Ctrl Pts',(20.2723746104174,-16.9829351996645,
4.19318901775914));
#213370=CARTESIAN_POINT('Ctrl Pts',(21.2223648848585,-19.179712164146,4.32036482444056));
#213371=CARTESIAN_POINT('Ctrl Pts',(19.8894348227856,-21.1675773514354,
4.44754063112201));
#213372=CARTESIAN_POINT('Ctrl Pts',(17.4964650251793,-21.1227878330214,
4.57471643780344));
#213373=CARTESIAN_POINT('Ctrl Pts',(16.2388567568882,-19.0864352120986,
4.70189224448488));
#213374=CARTESIAN_POINT('Ctrl Pts',(17.2703875480967,-16.9267466280655,
4.8290680511663));
#213375=CARTESIAN_POINT('Ctrl Pts',(19.6446919218926,-16.6251023113816,
4.95624385784775));
#213376=CARTESIAN_POINT('Ctrl Pts',(21.1834929812674,-18.4582422004466,
5.08341966452918));
#213377=CARTESIAN_POINT('Ctrl Pts',(20.4750362630098,-20.7443742245365,
5.21059547121061));
#213378=CARTESIAN_POINT('Ctrl Pts',(18.1692868343382,-21.386114144905,5.33777127789205));
#213379=CARTESIAN_POINT('Ctrl Pts',(16.3816266851093,-19.7947054154853,
5.46494708457348));
#213380=CARTESIAN_POINT('Ctrl Pts',(16.7521230475383,-17.4301667715549,
5.59212289125491));
#213381=CARTESIAN_POINT('Ctrl Pts',(18.9408685046945,-16.4618156591,5.71929869793635));
#213382=CARTESIAN_POINT('Ctrl Pts',(20.9398249485008,-17.7780541211498,
5.84647450461778));
#213383=CARTESIAN_POINT('Ctrl Pts',(20.9150739109944,-20.1713150637459,
5.97365031129922));
#213384=CARTESIAN_POINT('Ctrl Pts',(18.8893229328647,-21.4459301145832,
6.10082611798065));
#213385=CARTESIAN_POINT('Ctrl Pts',(16.7210728042601,-20.4325190760503,
6.22800192466209));
#213386=CARTESIAN_POINT('Ctrl Pts',(16.3995584413949,-18.0608236766186,
6.35517773134351));
#213387=CARTESIAN_POINT('Ctrl Pts',(18.2197493167659,-16.5067272412486,
6.48235353802496));
#213388=CARTESIAN_POINT('Ctrl Pts',(20.5117332760072,-17.1960167912891,
6.60952934470639));
#213389=CARTESIAN_POINT('Ctrl Pts',(21.1727572930827,-19.4963119467122,
6.73670515138783));
#213390=CARTESIAN_POINT('Ctrl Pts',(19.5963728601034,-21.2972346748364,
6.86388095806926));
#213391=CARTESIAN_POINT('Ctrl Pts',(17.2288148528754,-20.9465501504785,
6.99105676475069));
#213392=CARTESIAN_POINT('Ctrl Pts',(16.2421707958078,-18.7659896588004,
7.11823257143212));
#213393=CARTESIAN_POINT('Ctrl Pts',(17.5416253732237,-16.7560821100692,
7.24540837811357));
#213394=CARTESIAN_POINT('Ctrl Pts',(19.935009663591,-16.7607929313141,7.37258418479499));
#213395=CARTESIAN_POINT('Ctrl Pts',(21.2265421306802,-18.7758002364295,
7.49975999147643));
#213396=CARTESIAN_POINT('Ctrl Pts',(20.2313218974823,-20.9524598884302,
7.62693579815786));
#213397=CARTESIAN_POINT('Ctrl Pts',(17.8624017576224,-21.2938217553397,
7.7541116048393));
#213398=CARTESIAN_POINT('Ctrl Pts',(16.2931189076558,-19.4867075115756,
7.88128741152073));
#213399=CARTESIAN_POINT('Ctrl Pts',(16.9631929617487,-17.189032313632,8.00846321820217));
#213400=CARTESIAN_POINT('Ctrl Pts',(19.2578725647568,-16.5087705458158,
8.1356390248836));
#213401=CARTESIAN_POINT('Ctrl Pts',(21.0719316047989,-18.0700201582916,
8.26281483156504));
#213402=CARTESIAN_POINT('Ctrl Pts',(20.7410835058385,-20.440431533692,8.38999063824647));
#213403=CARTESIAN_POINT('Ctrl Pts',(18.5688608639229,-21.4452993594099,
8.5171664449279));
#213404=CARTESIAN_POINT('Ctrl Pts',(16.5481431296672,-20.1627197744802,
8.64434225160934));
#213405=CARTESIAN_POINT('Ctrl Pts',(16.5328134043638,-17.7693799422089,
8.77151805829078));
#213406=CARTESIAN_POINT('Ctrl Pts',(18.5369357595085,-16.461020611282,8.89869386497221));
#213407=CARTESIAN_POINT('Ctrl Pts',(20.7218523241179,-17.4379802618865,
9.02586967165363));
#213408=CARTESIAN_POINT('Ctrl Pts',(21.0830377613791,-19.8039590515472,
9.15304547833508));
#213409=CARTESIAN_POINT('Ctrl Pts',(19.2891268503013,-21.3883182899558,
9.28022128501651));
#213410=CARTESIAN_POINT('Ctrl Pts',(16.9859215091302,-20.7375067122967,
9.40739709169795));
#213411=CARTESIAN_POINT('Ctrl Pts',(16.2864696853447,-18.4486035471503,
9.53457289837939));
#213412=CARTESIAN_POINT('Ctrl Pts',(17.8324750143917,-16.621535383186,9.6617487050608));
#213413=CARTESIAN_POINT('Ctrl Pts',(20.2055735627831,-16.9325238602014,
9.78892451174226));
#213414=CARTESIAN_POINT('Ctrl Pts',(21.2285947034771,-19.0962563526568,
9.91610031842368));
#213415=CARTESIAN_POINT('Ctrl Pts',(19.9629800357399,-21.1276425951086,
10.0432761251051));
#213416=CARTESIAN_POINT('Ctrl Pts',(17.569852464315,-21.1630117921569,10.1704519317865));
#213417=CARTESIAN_POINT('Ctrl Pts',(16.2447580017361,-19.1699149007699,
10.297627738468));
#213418=CARTESIAN_POINT('Ctrl Pts',(17.2033885727816,-16.9768946132505,
10.4248035451494));
#213419=CARTESIAN_POINT('Ctrl Pts',(19.5662601278407,-16.5959109292081,
10.5519793518308));
#213420=CARTESIAN_POINT('Ctrl Pts',(21.1655846714952,-18.3764927322373,
10.6791551585123));
#213421=CARTESIAN_POINT('Ctrl Pts',(20.5340812002182,-20.6850667334291,
10.8063309651937));
#213422=CARTESIAN_POINT('Ctrl Pts',(18.2511149533807,-21.4036595729525,
10.9335067718751));
#213423=CARTESIAN_POINT('Ctrl Pts',(16.4111657655901,-19.8730069214463,
11.0606825785565));
#213424=CARTESIAN_POINT('Ctrl Pts',(16.7022728165186,-17.4973875836496,
11.187858385238));
#213425=CARTESIAN_POINT('Ctrl Pts',(18.8573634550803,-16.4562848544257,
11.3150341919194));
#213426=CARTESIAN_POINT('Ctrl Pts',(20.8992757804055,-17.7048458697147,
11.4422099986009));
#213427=CARTESIAN_POINT('Ctrl Pts',(20.9546819693801,-20.0975933924253,
11.5693858052823));
#213428=CARTESIAN_POINT('Ctrl Pts',(18.9727502825159,-21.4393300811306,
11.6965616119637));
#213429=CARTESIAN_POINT('Ctrl Pts',(16.7717800299571,-20.4990958015143,
11.8237374186452));
#213430=CARTESIAN_POINT('Ctrl Pts',(16.3710248108061,-18.1394971476037,
11.9509132253266));
#213431=CARTESIAN_POINT('Ctrl Pts',(18.1381526649597,-16.5253194311522,
12.078089032008));
#213432=CARTESIAN_POINT('Ctrl Pts',(20.4519334665563,-17.137470519836,12.2052648386895));
#213433=CARTESIAN_POINT('Ctrl Pts',(21.1896169395636,-19.4143397841694,
12.3324406453709));
#213434=CARTESIAN_POINT('Ctrl Pts',(19.6744242832976,-21.2670409925706,
12.4596164520523));
#213435=CARTESIAN_POINT('Ctrl Pts',(17.2964507164197,-20.9958357779372,
12.5867922587338));
#213436=CARTESIAN_POINT('Ctrl Pts',(16.2373393928556,-18.8495380918013,
12.7139680654152));
#213437=CARTESIAN_POINT('Ctrl Pts',(17.4687592161129,-16.7972428469345,
12.8411438720966));
#213438=CARTESIAN_POINT('Ctrl Pts',(19.8609589288869,-16.7218035506933,
12.9683196787781));
#213439=CARTESIAN_POINT('Ctrl Pts',(21.219243771367,-18.6924310750883,13.0954954854595));
#213440=CARTESIAN_POINT('Ctrl Pts',(20.2974717052425,-20.9011969774254,
13.222671292141));
#213441=CARTESIAN_POINT('Ctrl Pts',(17.9413113895561,-21.3216956337831,
13.3498470988224));
#213442=CARTESIAN_POINT('Ctrl Pts',(16.3123936741481,-19.5681456260435,
13.4770229055038));
#213443=CARTESIAN_POINT('Ctrl Pts',(16.9051494608696,-17.2493202487194,
13.6041987121852));
#213444=CARTESIAN_POINT('Ctrl Pts',(19.1757621059772,-16.4925978629714,
13.7313745188667));
#213445=CARTESIAN_POINT('Ctrl Pts',(21.0410854376991,-17.9922242902351,
13.8585503255481));
#213446=CARTESIAN_POINT('Ctrl Pts',(20.7898010742036,-20.3723853608092,
13.9857261322295));
#213447=CARTESIAN_POINT('Ctrl Pts',(18.6524468225313,-21.449431021899,14.112901938911));
#213448=CARTESIAN_POINT('Ctrl Pts',(16.5899125494253,-20.2352387284471,
14.2400777455924));
#213449=CARTESIAN_POINT('Ctrl Pts',(16.4944454351462,-17.8437545484231,
14.3672535522739));
#213450=CARTESIAN_POINT('Ctrl Pts',(18.4536306316875,-16.4690167847506,
14.4944293589553));
#213451=CARTESIAN_POINT('Ctrl Pts',(20.67003732197,-17.3722620097506,14.6216051656367));
#213452=CARTESIAN_POINT('Ctrl Pts',(21.1102499333731,-19.7248187912068,
14.7487809723181));
#213453=CARTESIAN_POINT('Ctrl Pts',(19.3704007176107,-21.3683622982746,
14.8759567789996));
#213454=CARTESIAN_POINT('Ctrl Pts',(17.0466933429237,-20.7950433730338,
15.003132585681));
#213455=CARTESIAN_POINT('Ctrl Pts',(16.2709851000421,-18.5308465452073,
15.1303083923625));
#213456=CARTESIAN_POINT('Ctrl Pts',(17.7549401559266,-16.6530318724217,
15.2574841990439));
#213457=CARTESIAN_POINT('Ctrl Pts',(20.137121851441,-16.8843777666347,15.3846600057253));
#213458=CARTESIAN_POINT('Ctrl Pts',(21.2320263358222,-19.0126387288515,
15.5118358124068));
#213459=CARTESIAN_POINT('Ctrl Pts',(20.0351467020866,-21.085267421011,15.6390116190882));
#213460=CARTESIAN_POINT('Ctrl Pts',(17.6445457274587,-21.2007556599016,
15.7661874257696));
#213461=CARTESIAN_POINT('Ctrl Pts',(16.2534514287292,-19.2531501543497,
15.893363232451));
#213462=CARTESIAN_POINT('Ctrl Pts',(17.1381064839328,-17.0292580736685,
16.0205390391325));
#213463=CARTESIAN_POINT('Ctrl Pts',(19.4868947878054,-16.5693623715735,
16.1477148458139));
#213464=CARTESIAN_POINT('Ctrl Pts',(21.1449488537871,-18.2953888103906,
16.2748906524954));
#213465=CARTESIAN_POINT('Ctrl Pts',(20.5911069867814,-20.6238152617876,
16.4020664591768));
#213466=CARTESIAN_POINT('Ctrl Pts',(18.3334847244627,-21.4184549750521,
16.5292422658582));
#213467=CARTESIAN_POINT('Ctrl Pts',(16.4433103686679,-19.950275334167,16.6564180725397));
#213468=CARTESIAN_POINT('Ctrl Pts',(16.6547015733873,-17.5662400341386,
16.7835938792211));
#213469=CARTESIAN_POINT('Ctrl Pts',(18.7737200287087,-16.4535534928245,
16.9107696859025));
#213470=CARTESIAN_POINT('Ctrl Pts',(20.8562978229928,-17.633036550765,17.037945492584));
#213471=CARTESIAN_POINT('Ctrl Pts',(20.9917990893397,-20.0225867092743,
17.1651212992654));
#213472=CARTESIAN_POINT('Ctrl Pts',(19.0559098260331,-21.4299400101298,
17.2922971059468));
#213473=CARTESIAN_POINT('Ctrl Pts',(16.8246882773183,-20.563937149993,17.4194729126283));
#213474=CARTESIAN_POINT('Ctrl Pts',(16.3451417289135,-18.2190820028416,
17.5466487193097));
#213475=CARTESIAN_POINT('Ctrl Pts',(18.0572243749644,-16.5466336280595,
17.6738245259911));
#213476=CARTESIAN_POINT('Ctrl Pts',(20.3902066515531,-17.0809596056631,
17.8010003326726));
#213477=CARTESIAN_POINT('Ctrl Pts',(21.2037221211194,-19.3318490151982,
17.928176139354));
#213478=CARTESIAN_POINT('Ctrl Pts',(19.7514208328018,-21.2342505293946,
18.0553519460354));
#213479=CARTESIAN_POINT('Ctrl Pts',(17.3656990786459,-21.0428288352822,
18.1825277527169));
#213480=CARTESIAN_POINT('Ctrl Pts',(16.2353084935018,-18.9332014563341,
18.3097035593983));
#213481=CARTESIAN_POINT('Ctrl Pts',(17.3973122792794,-16.8408205743096,
18.4368793660797));
#213482=CARTESIAN_POINT('Ctrl Pts',(19.7856440846313,-16.6853157810153,
18.5640551727612));
#213483=CARTESIAN_POINT('Ctrl Pts',(21.2091577147082,-18.6093530719028,
18.6912309794426));
#213484=CARTESIAN_POINT('Ctrl Pts',(20.3618677671906,-20.8477476531151,
18.8184067861241));
#213485=CARTESIAN_POINT('Ctrl Pts',(18.0211101800729,-21.3469114243016,
18.9455825928055));
#213486=CARTESIAN_POINT('Ctrl Pts',(16.3343847559432,-19.6488926118612,
19.072758399487));
#213487=CARTESIAN_POINT('Ctrl Pts',(16.849157381052,-17.3115180758999,19.1999342061683));
#213488=CARTESIAN_POINT('Ctrl Pts',(19.0931561230287,-16.4791838974025,
19.3271100128498));
#213489=CARTESIAN_POINT('Ctrl Pts',(21.0076514128875,-17.9155049898426,
19.4542858195312));
#213490=CARTESIAN_POINT('Ctrl Pts',(20.8362126520363,-20.3027459661324,
19.5814616262127));
#213491=CARTESIAN_POINT('Ctrl Pts',(18.7361242573274,-21.4507612701356,
19.7086374328941));
#213492=CARTESIAN_POINT('Ctrl Pts',(16.6340869953943,-20.3063183634152,
19.8358132395755));
#213493=CARTESIAN_POINT('Ctrl Pts',(16.4585895663445,-17.9193721006837,
19.9629890462569));
#213494=CARTESIAN_POINT('Ctrl Pts',(18.3706400083713,-16.4797984525115,
20.0901648529384));
#213495=CARTESIAN_POINT('Ctrl Pts',(20.6160506397633,-17.3083151083569,
20.2173406596198));
#213496=CARTESIAN_POINT('Ctrl Pts',(21.1347967193193,-19.6448128954076,
20.3445164663014));
#213497=CARTESIAN_POINT('Ctrl Pts',(19.4509606323996,-21.3456934933219,
20.4716922729828));
#213498=CARTESIAN_POINT('Ctrl Pts',(17.1093580247237,-20.8505172793461,
20.5988680796641));
#213499=CARTESIAN_POINT('Ctrl Pts',(16.2582628992159,-18.6135531118782,
20.7260438863456));
#213500=CARTESIAN_POINT('Ctrl Pts',(17.6785042384983,-16.6871241470058,
20.853219693027));
#213501=CARTESIAN_POINT('Ctrl Pts',(20.0670948522008,-16.8385181003778,
20.9803954997085));
#213502=CARTESIAN_POINT('Ctrl Pts',(21.2326586430337,-18.9290163402638,
21.1075713063899));
#213503=CARTESIAN_POINT('Ctrl Pts',(20.1058486485267,-21.0403774658824,
21.2347471130713));
#213504=CARTESIAN_POINT('Ctrl Pts',(17.7204711065961,-21.2362120246932,
21.3619229197527));
#213505=CARTESIAN_POINT('Ctrl Pts',(16.264907789365,-19.3355946319105,21.4890987264342));
#213506=CARTESIAN_POINT('Ctrl Pts',(17.0746528505921,-17.0846536771093,
21.6162745331156));
#213507=CARTESIAN_POINT('Ctrl Pts',(19.4066037445858,-16.543775807204,21.743450339797));
#213508=CARTESIAN_POINT('Ctrl Pts',(21.1220855276092,-18.2187873983098,
21.8706448040796));
#213509=CARTESIAN_POINT('Ctrl Pts',(20.8038319347303,-19.7747688677855,
21.9554473328015));
#213510=CARTESIAN_POINT('Ctrl Pts',(20.3504142419353,-20.3131719366696,
21.9978579259631));
#213511=CARTESIAN_POINT('Ctrl Pts',(18.0722627314315,-21.4249949024184,
-8.32884108903365E-16));
#213512=CARTESIAN_POINT('Ctrl Pts',(17.9903580532758,-21.3953391176122,
1.14284362820775E-14));
#213513=CARTESIAN_POINT('Ctrl Pts',(17.9103568112513,-21.3612556170403,
1.33837946700833E-14));
#213514=CARTESIAN_POINT('Ctrl Pts',(17.8324629519401,-21.3230651201994,
-1.18308141061618E-15));
#213515=CARTESIAN_POINT('Ctrl Pts',(17.7532833251911,-21.2842442258188,
-1.59904079594309E-14));
#213516=CARTESIAN_POINT('Ctrl Pts',(17.676280547661,-21.2411789324049,-3.34052718883277E-15));
#213517=CARTESIAN_POINT('Ctrl Pts',(17.6016979156783,-21.1941602566529,
3.01494940124769E-15));
#213518=CARTESIAN_POINT('Ctrl Pts',(17.5268866858167,-21.1469974673284,
9.38990570702805E-15));
#213519=CARTESIAN_POINT('Ctrl Pts',(17.454509827292,-21.0958562232334,-7.05390108614649E-15));
#213520=CARTESIAN_POINT('Ctrl Pts',(17.3848517335724,-21.0409959625991,
-1.83394965880268E-14));
#213521=CARTESIAN_POINT('Ctrl Pts',(17.3596729290501,-21.0211660231794,
-2.24188187153734E-14));
#213522=CARTESIAN_POINT('Ctrl Pts',(17.3348497590451,-21.0008499098405,
-1.906235806488E-14));
#213523=CARTESIAN_POINT('Ctrl Pts',(17.3103971449292,-20.9800590889455,
-1.05540576278429E-14));
#213524=CARTESIAN_POINT('Ctrl Pts',(17.2929747331899,-20.9652456935222,
-4.68390922674883E-15));
#213525=CARTESIAN_POINT('Ctrl Pts',(17.2757404518089,-20.9501913039064,
-5.50447044822256E-16));
#213526=CARTESIAN_POINT('Ctrl Pts',(17.2586999683651,-20.9348999714627,
-1.45786160921091E-14));
#213527=CARTESIAN_POINT('Ctrl Pts',(17.2462568322336,-20.9237340833671,
-2.48221292944806E-14));
#213528=CARTESIAN_POINT('Ctrl Pts',(17.2339149535825,-20.9124397717598,
-2.54522446515586E-14));
#213529=CARTESIAN_POINT('Ctrl Pts',(17.2216943473019,-20.9010355554554,
-1.92693083711504E-14));
#213530=CARTESIAN_POINT('Ctrl Pts',(17.1582585289398,-20.8418375273512,
1.29026392568497E-14));
#213531=CARTESIAN_POINT('Ctrl Pts',(17.0979854521548,-20.7795917637398,
-1.84358832270529E-14));
#213532=CARTESIAN_POINT('Ctrl Pts',(17.0411057216722,-20.7145765131158,
-1.86101134502792E-14));
#213533=CARTESIAN_POINT('Ctrl Pts',(16.984562346582,-20.6499457268686,-1.87833133719448E-14));
#213534=CARTESIAN_POINT('Ctrl Pts',(16.9313717910639,-20.5825772843491,
-1.74089365841943E-14));
#213535=CARTESIAN_POINT('Ctrl Pts',(16.8818041708662,-20.5127177725604,
2.4980018054066E-16));
#213536=CARTESIAN_POINT('Ctrl Pts',(16.8334274591682,-20.4445367009721,
1.74842692555363E-14));
#213537=CARTESIAN_POINT('Ctrl Pts',(16.7885013791215,-20.3739820606686,
2.0753501284633E-15));
#213538=CARTESIAN_POINT('Ctrl Pts',(16.7473244499658,-20.3012692713251,
1.06858966120171E-15));
#213539=CARTESIAN_POINT('Ctrl Pts',(16.7339895188643,-20.2777216184046,
7.42555599363664E-16));
#213540=CARTESIAN_POINT('Ctrl Pts',(16.721048178709,-20.2539475653071,-1.12813719766283E-15));
#213541=CARTESIAN_POINT('Ctrl Pts',(16.708511751901,-20.2299543047592,1.70696790036118E-15));
#213542=CARTESIAN_POINT('Ctrl Pts',(16.6986550608892,-20.2110897463642,
3.81121037099786E-15));
#213543=CARTESIAN_POINT('Ctrl Pts',(16.689048690518,-20.1920896772321,-1.29321329154552E-14));
#213544=CARTESIAN_POINT('Ctrl Pts',(16.6796984128078,-20.1729575913137,
3.7470027081099E-15));
#213545=CARTESIAN_POINT('Ctrl Pts',(16.673772461475,-20.1608321963725,1.4257350817072E-14));
#213546=CARTESIAN_POINT('Ctrl Pts',(16.6679532034413,-20.1486615485784,
-2.13375587759138E-14));
#213547=CARTESIAN_POINT('Ctrl Pts',(16.6622433073212,-20.1364502099952,
-2.15105711021124E-14));
#213548=CARTESIAN_POINT('Ctrl Pts',(16.6271177740505,-20.0613297926252,
-2.27890517030476E-14));
#213549=CARTESIAN_POINT('Ctrl Pts',(16.596105677901,-19.9846276360536,1.38706764190184E-14));
#213550=CARTESIAN_POINT('Ctrl Pts',(16.5694538163414,-19.9065723114556,
7.48012762841199E-15));
#213551=CARTESIAN_POINT('Ctrl Pts',(16.5428019547817,-19.8285169868576,
4.05397723666108E-16));
#213552=CARTESIAN_POINT('Ctrl Pts',(16.5205098557042,-19.7491077644459,
-1.49783758356987E-14));
#213553=CARTESIAN_POINT('Ctrl Pts',(16.502878625203,-19.66856395302,-1.87350135405495E-14));
#213554=CARTESIAN_POINT('Ctrl Pts',(16.4850541528343,-19.5871373650609,
-2.27945971057644E-14));
#213555=CARTESIAN_POINT('Ctrl Pts',(16.4719940148662,-19.5045499555443,
-7.13018664987758E-15));
#213556=CARTESIAN_POINT('Ctrl Pts',(16.4636225525689,-19.4211931726568,
-1.67643676718399E-14));
#213557=CARTESIAN_POINT('Ctrl Pts',(16.4601640820937,-19.3867563010228,
-2.07983225502737E-14));
#213558=CARTESIAN_POINT('Ctrl Pts',(16.4575064389052,-19.3521882740751,
1.67910904244036E-14));
#213559=CARTESIAN_POINT('Ctrl Pts',(16.4556467099008,-19.3175176204782,
1.35447209004269E-14));
#213560=CARTESIAN_POINT('Ctrl Pts',(16.4549147504963,-19.3038718092329,
1.22971584021043E-14));
#213561=CARTESIAN_POINT('Ctrl Pts',(16.4543064087743,-19.2902081093511,
-1.28578812753533E-14));
#213562=CARTESIAN_POINT('Ctrl Pts',(16.4538219778623,-19.2765459176976,
-1.26842980563424E-14));
#213563=CARTESIAN_POINT('Ctrl Pts',(16.4509249680159,-19.194842824923,-1.16389388342459E-14));
#213564=CARTESIAN_POINT('Ctrl Pts',(16.4524464982906,-19.1130624309727,
-8.75788806185453E-15));
#213565=CARTESIAN_POINT('Ctrl Pts',(16.458252360817,-19.0315664983848,5.71764857681956E-15));
#213566=CARTESIAN_POINT('Ctrl Pts',(16.4640582233434,-18.9500705657969,
2.01931852154936E-14));
#213567=CARTESIAN_POINT('Ctrl Pts',(16.474148825966,-18.868858075135,-1.49069399145082E-14));
#213568=CARTESIAN_POINT('Ctrl Pts',(16.4884408456005,-18.7883024616738,
-1.04083408558608E-14));
#213569=CARTESIAN_POINT('Ctrl Pts',(16.5025319927713,-18.7088790468066,
-6.09247964456401E-15));
#213570=CARTESIAN_POINT('Ctrl Pts',(16.5207077570521,-18.6300932899197,
1.349074868505E-14));
#213571=CARTESIAN_POINT('Ctrl Pts',(16.5429310587135,-18.5523284952265,
-1.60982338570648E-15));
#213572=CARTESIAN_POINT('Ctrl Pts',(16.5522282722733,-18.5197952598546,
-7.77797097015512E-15));
#213573=CARTESIAN_POINT('Ctrl Pts',(16.5622343667201,-18.4874410976137,
-4.30226113493849E-15));
#213574=CARTESIAN_POINT('Ctrl Pts',(16.572948601838,-18.4552959778321,-1.75415237890775E-14));
#213575=CARTESIAN_POINT('Ctrl Pts',(16.578489270918,-18.4386727220153,-2.43817434326259E-14));
#213576=CARTESIAN_POINT('Ctrl Pts',(16.5842201970324,-18.4221033375436,
1.47432613954525E-14));
#213577=CARTESIAN_POINT('Ctrl Pts',(16.5901333946024,-18.4056133356731,
1.04360964314765E-14));
#213578=CARTESIAN_POINT('Ctrl Pts',(16.6168665563098,-18.3310631652543,
-9.14610413127907E-15));
#213579=CARTESIAN_POINT('Ctrl Pts',(16.6473525954954,-18.2580371498547,
-2.56830120342859E-14));
#213580=CARTESIAN_POINT('Ctrl Pts',(16.6815326594994,-18.186894548015,-5.8564264548977E-15));
#213581=CARTESIAN_POINT('Ctrl Pts',(16.7078448582386,-18.1321281708012,
9.40630272034479E-15));
#213582=CARTESIAN_POINT('Ctrl Pts',(16.7363470804512,-18.0784782971011,
1.13991640136532E-14));
#213583=CARTESIAN_POINT('Ctrl Pts',(16.7670276804213,-18.0261235050124,
7.49400541621981E-15));
#213584=CARTESIAN_POINT('Ctrl Pts',(16.7762619506765,-18.01036571997,6.10196084666463E-15));
#213585=CARTESIAN_POINT('Ctrl Pts',(16.7856936431618,-17.9947253587034,
-4.23954215232061E-15));
#213586=CARTESIAN_POINT('Ctrl Pts',(16.795322651707,-17.9792075715296,-2.24820162486594E-15));
#213587=CARTESIAN_POINT('Ctrl Pts',(16.8035475707392,-17.9659525679159,
-3.76426044640903E-16));
#213588=CARTESIAN_POINT('Ctrl Pts',(16.8119141895608,-17.9527907636739,
-4.11143789873392E-15));
#213589=CARTESIAN_POINT('Ctrl Pts',(16.8204178980527,-17.9397316712593,
-3.41393580072236E-15));
#213590=CARTESIAN_POINT('Ctrl Pts',(16.8615694249279,-17.8765355265444,
7.90562951105821E-16));
#213591=CARTESIAN_POINT('Ctrl Pts',(16.9059580734959,-17.8156943310143,
1.33637921099262E-14));
#213592=CARTESIAN_POINT('Ctrl Pts',(16.9535504683774,-17.7575478141846,
1.74860126378462E-15));
#213593=CARTESIAN_POINT('Ctrl Pts',(16.9976826813803,-17.7036288115269,
-9.07571888140078E-15));
#213594=CARTESIAN_POINT('Ctrl Pts',(17.044570268779,-17.6520267822693,9.32681404607894E-15));
#213595=CARTESIAN_POINT('Ctrl Pts',(17.0942091882108,-17.6030457893103,
4.27435864480685E-15));
#213596=CARTESIAN_POINT('Ctrl Pts',(17.0997977486715,-17.5975313010074,
3.76786346256753E-15));
#213597=CARTESIAN_POINT('Ctrl Pts',(17.10542120347,-17.592050073031,7.85802203456014E-15));
#213598=CARTESIAN_POINT('Ctrl Pts',(17.1110791840834,-17.5866022544178,
1.97064586870965E-14));
#213599=CARTESIAN_POINT('Ctrl Pts',(-17.1175855514924,-17.590827960842,
0.00214194799035405));
#213600=CARTESIAN_POINT('Ctrl Pts',(-16.6641678381752,-18.1292310858663,
0.0445525400540117));
#213601=CARTESIAN_POINT('Ctrl Pts',(-16.345912932243,-19.6852113602882,
0.129355067678147));
#213602=CARTESIAN_POINT('Ctrl Pts',(-18.0613969831487,-21.3602251232166,
0.256549530862762));
#213603=CARTESIAN_POINT('Ctrl Pts',(-20.393346844718,-20.8193459211516,
0.383725337544195));
#213604=CARTESIAN_POINT('Ctrl Pts',(-21.203092563641,-18.5684056721843,
0.510901144225632));
#213605=CARTESIAN_POINT('Ctrl Pts',(-19.7475288416972,-16.6677876400165,
0.638076950907064));
#213606=CARTESIAN_POINT('Ctrl Pts',(-17.3621513300928,-16.8636225363617,
0.765252757588499));
#213607=CARTESIAN_POINT('Ctrl Pts',(-16.2353411818156,-18.9749835879209,
0.892428564269934));
#213608=CARTESIAN_POINT('Ctrl Pts',(-17.4009050866724,-21.0654820647258,
1.01960437095136));
#213609=CARTESIAN_POINT('Ctrl Pts',(-19.7894958141682,-21.2168759594155,
1.1467801776328));
#213610=CARTESIAN_POINT('Ctrl Pts',(-21.2097372485274,-19.2904469218172,
1.27395598431423));
#213611=CARTESIAN_POINT('Ctrl Pts',(-20.3586420669921,-17.0534826027649,
1.40113179099567));
#213612=CARTESIAN_POINT('Ctrl Pts',(-18.0170393273216,-16.558306372611,
1.5283075976771));
#213613=CARTESIAN_POINT('Ctrl Pts',(-16.3332031410643,-18.2591870619742,
1.65548340435853));
#213614=CARTESIAN_POINT('Ctrl Pts',(-16.8519492516291,-20.5956849881885,
1.78265921103997));
#213615=CARTESIAN_POINT('Ctrl Pts',(-19.097360012485,-21.424201689821,1.9098350177214));
#213616=CARTESIAN_POINT('Ctrl Pts',(-21.0094105654639,-19.9846279595186,
2.03701082440284));
#213617=CARTESIAN_POINT('Ctrl Pts',(-20.8339131261131,-17.5976815579533,
2.16418663108427));
#213618=CARTESIAN_POINT('Ctrl Pts',(-18.7318757425753,-16.4532385853486,
2.29136243776571));
#213619=CARTESIAN_POINT('Ctrl Pts',(-16.6317872262606,-17.6012539556073,
2.41853824444714));
#213620=CARTESIAN_POINT('Ctrl Pts',(-16.460348455506,-19.9884950701948,
2.54571405112858));
#213621=CARTESIAN_POINT('Ctrl Pts',(-18.3748438561772,-21.4248162457191,
2.67288985781001));
#213622=CARTESIAN_POINT('Ctrl Pts',(-20.6188427280565,-20.592482019073,
2.80006566449145));
#213623=CARTESIAN_POINT('Ctrl Pts',(-21.1336153829609,-18.2551073477921,
2.92724147117288));
#213624=CARTESIAN_POINT('Ctrl Pts',(-19.4468898611942,-16.5570884370688,
3.05441727785431));
#213625=CARTESIAN_POINT('Ctrl Pts',(-17.1061321385776,-17.056252237145,
3.18159308453575));
#213626=CARTESIAN_POINT('Ctrl Pts',(-16.2588421420139,-19.2946469479328,
3.30876889121718));
#213627=CARTESIAN_POINT('Ctrl Pts',(-17.6823558544925,-21.2186843501945,
3.43594469789862));
#213628=CARTESIAN_POINT('Ctrl Pts',(-20.0706877980967,-21.0631795478994,
3.56312050458005));
#213629=CARTESIAN_POINT('Ctrl Pts',(-21.2326916511383,-18.970798544754,
3.69029631126149));
#213630=CARTESIAN_POINT('Ctrl Pts',(-20.1023010005601,-16.8611710436873,
3.81747211794292));
#213631=CARTESIAN_POINT('Ctrl Pts',(-17.7165791083032,-16.6697493384941,
3.94464792462435));
#213632=CARTESIAN_POINT('Ctrl Pts',(-16.2642777359172,-18.5721509628136,
4.07182373130579));
#213633=CARTESIAN_POINT('Ctrl Pts',(-17.077793252575,-20.8230405026448,
4.19899953798722));
#213634=CARTESIAN_POINT('Ctrl Pts',(-19.4107756642115,-21.3573665111786,
4.32617534466866));
#213635=CARTESIAN_POINT('Ctrl Pts',(-21.1228584093689,-19.6849180395844,
4.45335115135009));
#213636=CARTESIAN_POINT('Ctrl Pts',(-20.6433118332049,-17.3400627566978,
4.58052695803153));
#213637=CARTESIAN_POINT('Ctrl Pts',(-18.4120901553326,-16.474059846431,
4.70770276471296));
#213638=CARTESIAN_POINT('Ctrl Pts',(-16.4762007799643,-17.8814132287533,
4.8348785713944));
#213639=CARTESIAN_POINT('Ctrl Pts',(-16.6117020541549,-20.2709635255851,
4.96205437807583));
#213640=CARTESIAN_POINT('Ctrl Pts',(-18.694279968992,-21.4504466518017,
5.08923018475726));
#213641=CARTESIAN_POINT('Ctrl Pts',(-20.8132985469758,-20.3377600460781,
5.2164059914387));
#213642=CARTESIAN_POINT('Ctrl Pts',(-21.0246897639318,-17.9537246080465,
5.34358179812013));
#213643=CARTESIAN_POINT('Ctrl Pts',(-19.1345152987216,-16.4855448821736,
5.47075760480157));
#213644=CARTESIAN_POINT('Ctrl Pts',(-16.8768929057173,-17.2801846414369,
5.597933411483));
#213645=CARTESIAN_POINT('Ctrl Pts',(-16.3230510066515,-19.6086112276183,
5.72510921816443));
#213646=CARTESIAN_POINT('Ctrl Pts',(-17.9811051686122,-21.3346377663488,
5.85228502484587));
#213647=CARTESIAN_POINT('Ctrl Pts',(-20.3298936084476,-20.8747420376322,
5.97946083152731));
#213648=CARTESIAN_POINT('Ctrl Pts',(-21.2145487148608,-18.6508498282177,
6.10663663820873));
#213649=CARTESIAN_POINT('Ctrl Pts',(-19.8234543356058,-16.7032442099259,
6.23381244489018));
#213650=CARTESIAN_POINT('Ctrl Pts',(-17.4328532225945,-16.8187324555017,
6.36098825157161));
#213651=CARTESIAN_POINT('Ctrl Pts',(-16.2359735195759,-18.8913612676384,
6.48816405825305));
#213652=CARTESIAN_POINT('Ctrl Pts',(-17.3308780673371,-21.0196223530527,
6.61533986493447));
#213653=CARTESIAN_POINT('Ctrl Pts',(-19.7130599007477,-21.2509682606574,
6.74251567161592));
#213654=CARTESIAN_POINT('Ctrl Pts',(-21.1970150425329,-19.3731534791717,
6.86969147829734));
#213655=CARTESIAN_POINT('Ctrl Pts',(-20.4213067547485,-17.1089565202789,
6.99686728497878));
#213656=CARTESIAN_POINT('Ctrl Pts',(-18.0975992455503,-16.5356375618508,
7.12404309166021));
#213657=CARTESIAN_POINT('Ctrl Pts',(-16.3577499290741,-18.1791811640576,
7.25121889834165));
#213658=CARTESIAN_POINT('Ctrl Pts',(-16.7979625659597,-20.5317380816948,
7.37839470502308));
#213659=CARTESIAN_POINT('Ctrl Pts',(-19.014369384542,-21.4349833589804,
7.50557051170451));
#213660=CARTESIAN_POINT('Ctrl Pts',(-20.9735546944935,-20.0602455157292,
7.63274631838594));
#213661=CARTESIAN_POINT('Ctrl Pts',(-20.8780875746881,-17.6687611972708,
7.75992212506739));
#213662=CARTESIAN_POINT('Ctrl Pts',(-18.8155531821895,-16.4545688335337,
7.88709793174882));
#213663=CARTESIAN_POINT('Ctrl Pts',(-16.6781988067934,-17.5316145569697,
8.01427373843027));
#213664=CARTESIAN_POINT('Ctrl Pts',(-16.4269144287518,-19.9117757653229,
8.14144954511167));
#213665=CARTESIAN_POINT('Ctrl Pts',(-18.2922378684508,-21.4114022793946,
8.26862535179315));
#213666=CARTESIAN_POINT('Ctrl Pts',(-20.5628506449959,-20.6546798498427,
8.39580115847454));
#213667=CARTESIAN_POINT('Ctrl Pts',(-21.15560646603,-18.3358543382901,8.52297696515602));
#213668=CARTESIAN_POINT('Ctrl Pts',(-19.5266886563297,-16.5823042290437,
8.65015277183742));
#213669=CARTESIAN_POINT('Ctrl Pts',(-17.1705282042537,-17.0028029097426,
8.77732857851889));
#213670=CARTESIAN_POINT('Ctrl Pts',(-16.2487560847711,-19.2115689399372,
8.90450438520028));
#213671=CARTESIAN_POINT('Ctrl Pts',(-17.6070410058773,-21.1821965784047,
9.03168019188174));
#213672=CARTESIAN_POINT('Ctrl Pts',(-19.9992408571273,-21.1067572777967,
9.15885599856315));
#213673=CARTESIAN_POINT('Ctrl Pts',(-21.2306607516671,-19.0544619141298,
9.28603180524462));
#213674=CARTESIAN_POINT('Ctrl Pts',(-20.1715493667948,-16.9081641037524,
9.41320761192604));
#213675=CARTESIAN_POINT('Ctrl Pts',(-17.7935756622645,-16.6369588734199,
9.54038341860746));
#213676=CARTESIAN_POINT('Ctrl Pts',(-16.2783829182894,-18.4896601890674,
9.66755922528891));
#213677=CARTESIAN_POINT('Ctrl Pts',(-17.0160664339986,-20.7665295852005,
9.79473503197033));
#213678=CARTESIAN_POINT('Ctrl Pts',(-19.3298473695317,-21.3786807093197,
9.92191083865178));
#213679=CARTESIAN_POINT('Ctrl Pts',(-21.0969753259781,-19.7645028994292,
10.0490866453332));
#213680=CARTESIAN_POINT('Ctrl Pts',(-20.6962200836287,-17.4049041089298,
10.1762624520146));
#213681=CARTESIAN_POINT('Ctrl Pts',(-18.4952497036636,-16.4646697748868,
10.3034382586961));
#213682=CARTESIAN_POINT('Ctrl Pts',(-16.5133179020725,-17.8064065412604,
10.4306140653775));
#213683=CARTESIAN_POINT('Ctrl Pts',(-16.5687240942544,-20.1991542024786,
10.5577898720589));
#213684=CARTESIAN_POINT('Ctrl Pts',(-18.6106365377785,-21.4477152900423,
10.6849656787404));
#213685=CARTESIAN_POINT('Ctrl Pts',(-20.7657273010908,-20.4066125005527,
10.8121414854218));
#213686=CARTESIAN_POINT('Ctrl Pts',(-21.0568343688704,-18.0309930252399,
10.9393172921033));
#213687=CARTESIAN_POINT('Ctrl Pts',(-19.2168850745718,-16.5003402851297,
11.0664930987847));
#213688=CARTESIAN_POINT('Ctrl Pts',(-16.9339186955814,-17.2189331662498,
11.1936689054661));
#213689=CARTESIAN_POINT('Ctrl Pts',(-16.302415187749,-19.5275073010768,
11.3208447121476));
#213690=CARTESIAN_POINT('Ctrl Pts',(-17.9017398239826,-21.3080892071774,
11.448020518829));
#213691=CARTESIAN_POINT('Ctrl Pts',(-20.26461151582,-20.9271055010812,11.5751963255104));
#213692=CARTESIAN_POINT('Ctrl Pts',(-21.2232421423571,-18.7340850866159,
11.7023721321919));
#213693=CARTESIAN_POINT('Ctrl Pts',(-19.8981476030732,-16.7409880798555,
11.8295479388733));
#213694=CARTESIAN_POINT('Ctrl Pts',(-17.5050198931187,-16.7763572789512,
11.9567237455547));
#213695=CARTESIAN_POINT('Ctrl Pts',(-16.2394051521196,-18.8077436389928,
12.0838995522362));
#213696=CARTESIAN_POINT('Ctrl Pts',(-17.2624263520327,-20.9714762566988,
12.2110753589176));
#213697=CARTESIAN_POINT('Ctrl Pts',(-19.6355250377943,-21.2824647517163,
12.3382511655991));
#213698=CARTESIAN_POINT('Ctrl Pts',(-21.181530456334,-19.4553964819894,
12.4654269722804));
#213699=CARTESIAN_POINT('Ctrl Pts',(-20.4820785920598,-17.1664931843466,
12.5926027789619));
#213700=CARTESIAN_POINT('Ctrl Pts',(-18.1788731175643,-16.5156815690145,
12.7197785856433));
#213701=CARTESIAN_POINT('Ctrl Pts',(-16.3849621026435,-18.1000408991359,
12.8469543923248));
#213702=CARTESIAN_POINT('Ctrl Pts',(-16.7461475608124,-20.4660198257546,
12.9741301990062));
#213703=CARTESIAN_POINT('Ctrl Pts',(-18.9310642518988,-21.4429795329118,
13.1013060056876));
#213704=CARTESIAN_POINT('Ctrl Pts',(-20.9351867230549,-20.1346201262487,
13.2284818123691));
#213705=CARTESIAN_POINT('Ctrl Pts',(-20.9198569968642,-17.7412801554356,
13.3556576190505));
#213706=CARTESIAN_POINT('Ctrl Pts',(-18.8991391456364,-16.4587004962619,
13.4828334257319));
#213707=CARTESIAN_POINT('Ctrl Pts',(-16.7269163779785,-17.463568380148,
13.6100092324134));
#213708=CARTESIAN_POINT('Ctrl Pts',(-16.3960682598664,-19.8339798927631,
13.7371850390948));
#213709=CARTESIAN_POINT('Ctrl Pts',(-18.210127404918,-21.395229595614,13.8643608457763));
#213710=CARTESIAN_POINT('Ctrl Pts',(-20.5048071407569,-20.71496778842,13.9915366524577));
#213711=CARTESIAN_POINT('Ctrl Pts',(-21.174881233638,-18.417292457472,14.1187124591391));
#213712=CARTESIAN_POINT('Ctrl Pts',(-19.6055982928313,-16.6101781091006,
14.2458882658205));
#213713=CARTESIAN_POINT('Ctrl Pts',(-17.236678015843,-16.9515399957704,
14.373064072502));
#213714=CARTESIAN_POINT('Ctrl Pts',(-16.2414577250354,-19.12819977377,14.5002398791834));
#213715=CARTESIAN_POINT('Ctrl Pts',(-17.5329902668867,-21.1432071955271,
14.6274156858649));
#213716=CARTESIAN_POINT('Ctrl Pts',(-19.9263746957985,-21.1479180170447,
14.7545914925463));
#213717=CARTESIAN_POINT('Ctrl Pts',(-21.2258293484353,-19.1380103519671,
14.8817672992277));
#213718=CARTESIAN_POINT('Ctrl Pts',(-20.2391852342543,-16.9574497340641,
15.0089431059091));
#213719=CARTESIAN_POINT('Ctrl Pts',(-17.8716270899769,-16.6067651894063,
15.1361189125906));
#213720=CARTESIAN_POINT('Ctrl Pts',(-16.2952425657462,-18.4076880217795,
15.263294719272));
#213721=CARTESIAN_POINT('Ctrl Pts',(-16.9562666210861,-20.7079833103585,
15.3904705259535));
#213722=CARTESIAN_POINT('Ctrl Pts',(-19.2482507130021,-21.3972729002994,
15.5176463326349));
#213723=CARTESIAN_POINT('Ctrl Pts',(-21.0684416937376,-19.8431763749684,
15.6448221393163));
#213724=CARTESIAN_POINT('Ctrl Pts',(-20.746927312261,-17.4714808382477,
15.7719979459977));
#213725=CARTESIAN_POINT('Ctrl Pts',(-18.5786770581442,-16.4580697410522,
15.8991737526792));
#213726=CARTESIAN_POINT('Ctrl Pts',(-16.552925962751,-17.7326848656722,
16.0263495593606));
#213727=CARTESIAN_POINT('Ctrl Pts',(-16.5281749238118,-20.1259459468057,
16.1535253660421));
#213728=CARTESIAN_POINT('Ctrl Pts',(-18.5271314833305,-21.4421844850479,
16.2807011727235));
#213729=CARTESIAN_POINT('Ctrl Pts',(-20.7158770671853,-20.4738333165386,
16.4078769794049));
#213730=CARTESIAN_POINT('Ctrl Pts',(-21.0863734510612,-18.1092945357334,
16.5350527860864));
#213731=CARTESIAN_POINT('Ctrl Pts',(-19.298713198351,-16.5178857141929,
16.6622285927678));
#213732=CARTESIAN_POINT('Ctrl Pts',(-16.9929636362077,-17.1596256717093,
16.7894043994492));
#213733=CARTESIAN_POINT('Ctrl Pts',(-16.2845068769401,-19.4457578281354,
16.9165802061307));
#213734=CARTESIAN_POINT('Ctrl Pts',(-17.8233080253906,-21.2788978233141,
17.0437560128121));
#213735=CARTESIAN_POINT('Ctrl Pts',(-20.1976125366265,-20.9772534891692,
17.1709318194935));
#213736=CARTESIAN_POINT('Ctrl Pts',(-21.2291433875466,-18.8175647801194,
17.298107626175));
#213737=CARTESIAN_POINT('Ctrl Pts',(-19.9715350464571,-16.7812120413194,
17.4252834328564));
#213738=CARTESIAN_POINT('Ctrl Pts',(-17.5785651103304,-16.7364225203127,
17.5524592395378));
#213739=CARTESIAN_POINT('Ctrl Pts',(-16.2456349710989,-18.7242878226724,
17.6796350462193));
#213740=CARTESIAN_POINT('Ctrl Pts',(-17.1956253005315,-20.9210649143176,
17.8068108529007));
#213741=CARTESIAN_POINT('Ctrl Pts',(-19.5569789344254,-21.31134716103,17.9339866595822));
#213742=CARTESIAN_POINT('Ctrl Pts',(-21.163300475815,-19.5370748250935,
18.0611624662636));
#213743=CARTESIAN_POINT('Ctrl Pts',(-20.5408896100412,-17.2260326509801,
18.188338272945));
#213744=CARTESIAN_POINT('Ctrl Pts',(-18.2607696752627,-16.4984583939631,
18.3155140796264));
#213745=CARTESIAN_POINT('Ctrl Pts',(-16.4148091914615,-18.0218562765459,
18.4426898863079));
#213746=CARTESIAN_POINT('Ctrl Pts',(-16.6965623292452,-20.3986032941145,
18.5698656929893));
#213747=CARTESIAN_POINT('Ctrl Pts',(-18.8475380723677,-21.4481815757617,
18.6970414996708));
#213748=CARTESIAN_POINT('Ctrl Pts',(-20.894349680935,-20.2076681919521,
18.8242173063522));
#213749=CARTESIAN_POINT('Ctrl Pts',(-20.9591745439093,-17.8151571779635,
18.9513931130336));
#213750=CARTESIAN_POINT('Ctrl Pts',(-18.9825398722896,-16.4656288920389,
19.078568919715));
#213751=CARTESIAN_POINT('Ctrl Pts',(-16.7778852948647,-17.3971917774822,
19.2057447263965));
#213752=CARTESIAN_POINT('Ctrl Pts',(-16.3678445475033,-19.7551947020895,
19.3329205330779));
#213753=CARTESIAN_POINT('Ctrl Pts',(-18.1286045709649,-21.3763163446451,
19.4600963397593));
#213754=CARTESIAN_POINT('Ctrl Pts',(-20.4447773190769,-20.773278200954,
19.5872721464408));
#213755=CARTESIAN_POINT('Ctrl Pts',(-21.1914180721045,-18.4993303685776,
19.7144479531222));
#213756=CARTESIAN_POINT('Ctrl Pts',(-19.6835302447416,-16.6406787897749,
19.8416237598037));
#213757=CARTESIAN_POINT('Ctrl Pts',(-17.304507398182,-16.9025210366613,
19.9687995664851));
#213758=CARTESIAN_POINT('Ctrl Pts',(-16.2369552011117,-19.0446328885181,
20.0959753731665));
#213759=CARTESIAN_POINT('Ctrl Pts',(-17.4602867931939,-21.1017600821981,
20.223151179848));
#213760=CARTESIAN_POINT('Ctrl Pts',(-19.8521708689288,-21.1866153140319,
20.3503269865294));
#213761=CARTESIAN_POINT('Ctrl Pts',(-21.2182032059767,-19.221350684525,
20.4775027932109));
#213762=CARTESIAN_POINT('Ctrl Pts',(-20.3051320707828,-17.0089716056813,
20.6046785998922));
#213763=CARTESIAN_POINT('Ctrl Pts',(-17.9506471225061,-16.5792041686457,
20.7318544065737));
#213764=CARTESIAN_POINT('Ctrl Pts',(-16.3148352980017,-18.3263225287329,
20.8590302132551));
#213765=CARTESIAN_POINT('Ctrl Pts',(-16.8984656481068,-20.647474826016,
20.9862060199366));
#213766=CARTESIAN_POINT('Ctrl Pts',(-19.1660680562885,-21.4131078237249,
21.113381826618));
#213767=CARTESIAN_POINT('Ctrl Pts',(-21.0373071781416,-19.9208779742462,
21.2405576332995));
#213768=CARTESIAN_POINT('Ctrl Pts',(-20.7953426154092,-17.5396647859301,
21.3677334399809));
#213769=CARTESIAN_POINT('Ctrl Pts',(-18.6623441981192,-16.4543701936005,
21.4949092466623));
#213770=CARTESIAN_POINT('Ctrl Pts',(-16.5948542065943,-17.6601323237235,
21.6220850533437));
#213771=CARTESIAN_POINT('Ctrl Pts',(-16.4903435139124,-20.0518037409453,
21.7492608600252));
#213772=CARTESIAN_POINT('Ctrl Pts',(-18.4433885276789,-21.4331202535291,
21.8764366667066));
#213773=CARTESIAN_POINT('Ctrl Pts',(-20.6647168408145,-20.5407968853708,
22.0036124733881));
#213774=CARTESIAN_POINT('Ctrl Pts',(-21.1114425640841,-18.1855248151863,
22.1307882800695));
#213775=CARTESIAN_POINT('Ctrl Pts',(-19.9599076846608,-17.0924953497883,
22.2155721511904));
#213776=CARTESIAN_POINT('Ctrl Pts',(-19.2802416510892,-16.9106266592565,
22.2579640867509));
#213777=CARTESIAN_POINT('Ctrl Pts',(-17.0028272034401,-17.4941907062238,
-0.0844764445356067));
#213778=CARTESIAN_POINT('Ctrl Pts',(-16.5172188178569,-18.0708180956198,
-0.042065852471949));
#213779=CARTESIAN_POINT('Ctrl Pts',(-16.1763692071458,-19.7372661563571,
0.042736675152187));
#213780=CARTESIAN_POINT('Ctrl Pts',(-18.0136451140781,-21.531198562073,
0.169931138336801));
#213781=CARTESIAN_POINT('Ctrl Pts',(-20.5111532049132,-20.9519193050085,
0.297106945018235));
#213782=CARTESIAN_POINT('Ctrl Pts',(-21.3783873242474,-18.5411721545534,
0.424282751699669));
#213783=CARTESIAN_POINT('Ctrl Pts',(-19.8194849515203,-16.5056185643353,
0.551458558381104));
#213784=CARTESIAN_POINT('Ctrl Pts',(-17.2647560814413,-16.7153568808188,
0.678634365062538));
#213785=CARTESIAN_POINT('Ctrl Pts',(-16.0579473465983,-18.9766153220251,
0.805810171743973));
#213786=CARTESIAN_POINT('Ctrl Pts',(-17.306261185047,-21.2155300370204,
0.932985978425408));
#213787=CARTESIAN_POINT('Ctrl Pts',(-19.8644313952761,-21.3776722353249,
1.06016178510684));
#213788=CARTESIAN_POINT('Ctrl Pts',(-21.3855037526656,-19.3144751713091,
1.18733759178828));
#213789=CARTESIAN_POINT('Ctrl Pts',(-20.4739845399306,-16.9186961805966,
1.31451339846971));
#213790=CARTESIAN_POINT('Ctrl Pts',(-17.9661382589161,-16.3883646063293,
1.44168920515115));
#213791=CARTESIAN_POINT('Ctrl Pts',(-16.1627570764457,-18.2100003769934,
1.56886501183258));
#213792=CARTESIAN_POINT('Ctrl Pts',(-16.7183318894278,-20.7123794251487,
1.69604081851402));
#213793=CARTESIAN_POINT('Ctrl Pts',(-19.1231569823275,-21.5997171847722,
1.82321662519545));
#213794=CARTESIAN_POINT('Ctrl Pts',(-21.1709547522747,-20.0579400230779,
1.95039243187689));
#213795=CARTESIAN_POINT('Ctrl Pts',(-20.9829977631806,-17.5015308787203,
2.07756823855832));
#213796=CARTESIAN_POINT('Ctrl Pts',(-18.7317249295996,-16.2758374662316,
2.20474404523976));
#213797=CARTESIAN_POINT('Ctrl Pts',(-16.4825393242813,-17.5053569009653,
2.33191985192118));
#213798=CARTESIAN_POINT('Ctrl Pts',(-16.2989291514817,-20.062081681679,
2.45909565860262));
#213799=CARTESIAN_POINT('Ctrl Pts',(-18.3493453426023,-21.6003753714481,
2.58627146528406));
#213800=CARTESIAN_POINT('Ctrl Pts',(-20.7526583085904,-20.708949059251,
2.71344727196549));
#213801=CARTESIAN_POINT('Ctrl Pts',(-21.3039775679586,-18.2056310209682,
2.84062307864693));
#213802=CARTESIAN_POINT('Ctrl Pts',(-19.4975019198092,-16.3870602026966,
2.96779888532836));
#213803=CARTESIAN_POINT('Ctrl Pts',(-16.9905606483594,-16.9216624468904,
3.09497469200979));
#213804=CARTESIAN_POINT('Ctrl Pts',(-16.0831167720671,-19.3189733808883,
3.22215049869123));
#213805=CARTESIAN_POINT('Ctrl Pts',(-17.6076937249943,-21.3796090139306,
3.34932630537266));
#213806=CARTESIAN_POINT('Ctrl Pts',(-20.1655867788085,-21.2130640515812,
3.4765021120541));
#213807=CARTESIAN_POINT('Ctrl Pts',(-21.4100878173515,-18.9721331591185,
3.60367791873553));
#213808=CARTESIAN_POINT('Ctrl Pts',(-20.1994443802222,-16.7127313428988,
3.73085372541697));
#213809=CARTESIAN_POINT('Ctrl Pts',(-17.6443466799723,-16.507719534815,
3.8580295320984));
#213810=CARTESIAN_POINT('Ctrl Pts',(-16.0889382693367,-18.545183344418,
3.98520533877984));
#213811=CARTESIAN_POINT('Ctrl Pts',(-16.9602098255379,-20.95587618561,4.11238114546127));
#213812=CARTESIAN_POINT('Ctrl Pts',(-19.458823772974,-21.5281370010973,
4.2395569521427));
#213813=CARTESIAN_POINT('Ctrl Pts',(-21.2924568963431,-19.7369520111678,
4.36673275882414));
#213814=CARTESIAN_POINT('Ctrl Pts',(-20.7788646130614,-17.2256222706107,
4.49390856550557));
#213815=CARTESIAN_POINT('Ctrl Pts',(-18.3892359659074,-16.2981369456807,
4.62108437218701));
#213816=CARTESIAN_POINT('Ctrl Pts',(-16.3159069215641,-17.8054062557716,
4.74826017886844));
#213817=CARTESIAN_POINT('Ctrl Pts',(-16.4610281929029,-20.3646041605579,
4.87543598554988));
#213818=CARTESIAN_POINT('Ctrl Pts',(-18.6914600207125,-21.6278254241348,
5.00261179223131));
#213819=CARTESIAN_POINT('Ctrl Pts',(-20.9609196391894,-20.436142941524,
5.12978759891275));
#213820=CARTESIAN_POINT('Ctrl Pts',(-21.187318706931,-17.8828514263649,
5.25696340559418));
#213821=CARTESIAN_POINT('Ctrl Pts',(-19.1629501311951,-16.3104373686715,
5.38413921227561));
#213822=CARTESIAN_POINT('Ctrl Pts',(-16.7450464337355,-17.1614930713546,
5.51131501895704));
#213823=CARTESIAN_POINT('Ctrl Pts',(-16.1518841849429,-19.6552277496765,
5.63849082563848));
#213824=CARTESIAN_POINT('Ctrl Pts',(-17.9276529322832,-21.503794614907,
5.76566663231992));
#213825=CARTESIAN_POINT('Ctrl Pts',(-20.4431950667104,-21.0112483031962,
5.89284243900135));
#213826=CARTESIAN_POINT('Ctrl Pts',(-21.3906568120407,-18.629469484667,
6.02001824568278));
#213827=CARTESIAN_POINT('Ctrl Pts',(-19.9008008230416,-16.5435923954545,
6.14719405236422));
#213828=CARTESIAN_POINT('Ctrl Pts',(-17.3404774987283,-16.667279800778,
6.27436985904566));
#213829=CARTESIAN_POINT('Ctrl Pts',(-16.0586245775708,-18.8870561831594,
6.40154566572708));
#213830=CARTESIAN_POINT('Ctrl Pts',(-17.2312625539661,-21.1664144866242,
6.52872147240852));
#213831=CARTESIAN_POINT('Ctrl Pts',(-19.7825688666926,-21.414184940675,
6.65589727908996));
#213832=CARTESIAN_POINT('Ctrl Pts',(-21.3718783257522,-19.4030535320888,
6.78307308577139));
#213833=CARTESIAN_POINT('Ctrl Pts',(-20.5410981461279,-16.9781085033506,
6.91024889245283));
#213834=CARTESIAN_POINT('Ctrl Pts',(-18.0524175785914,-16.3640864092651,
7.03742469913425));
#213835=CARTESIAN_POINT('Ctrl Pts',(-16.1890465789213,-18.1243144106463,
7.1646005058157));
#213836=CARTESIAN_POINT('Ctrl Pts',(-16.6605123854672,-20.6438925682982,
7.29177631249713));
#213837=CARTESIAN_POINT('Ctrl Pts',(-19.0342743831914,-21.6112643052322,
7.41895211917856));
#213838=CARTESIAN_POINT('Ctrl Pts',(-21.1325532714676,-20.1389260946729,
7.54612792586));
#213839=CARTESIAN_POINT('Ctrl Pts',(-21.0303084041777,-17.5776568611929,
7.67330373254143));
#213840=CARTESIAN_POINT('Ctrl Pts',(-18.8213431010281,-16.277262156213,
7.80047953922286));
#213841=CARTESIAN_POINT('Ctrl Pts',(-16.5322459238095,-17.4307734099542,
7.92765534590431));
#213842=CARTESIAN_POINT('Ctrl Pts',(-16.2631214552256,-19.979915642092,
8.05483115258573));
#213843=CARTESIAN_POINT('Ctrl Pts',(-18.260874691454,-21.5860090722502,
8.18200695926717));
#213844=CARTESIAN_POINT('Ctrl Pts',(-20.6926910328048,-20.7755626636597,
8.30918276594861));
#213845=CARTESIAN_POINT('Ctrl Pts',(-21.3275299216332,-18.2921106942249,
8.43635857263003));
#213846=CARTESIAN_POINT('Ctrl Pts',(-19.5829660799844,-16.4140662054893,
8.56353437931147));
#213847=CARTESIAN_POINT('Ctrl Pts',(-17.0595285527274,-16.8644184512809,
8.69071018599291));
#213848=CARTESIAN_POINT('Ctrl Pts',(-16.0723146489239,-19.2299971980985,
8.81788599267433));
#213849=CARTESIAN_POINT('Ctrl Pts',(-17.5270318519084,-21.3405307701129,
8.94506179935578));
#213850=CARTESIAN_POINT('Ctrl Pts',(-20.089067417875,-21.2597356094876,
9.07223760603719));
#213851=CARTESIAN_POINT('Ctrl Pts',(-21.4079127329105,-19.0617362613832,
9.19941341271865));
#213852=CARTESIAN_POINT('Ctrl Pts',(-20.2736090772418,-16.7630607044602,
9.32658921940007));
#213853=CARTESIAN_POINT('Ctrl Pts',(-17.7268096521201,-16.4726010903001,
9.45376502608151));
#213854=CARTESIAN_POINT('Ctrl Pts',(-16.104044857895,-18.4568360869378,
9.58094083276294));
#213855=CARTESIAN_POINT('Ctrl Pts',(-16.8941006731258,-20.8953532404716,
9.70811663944438));
#213856=CARTESIAN_POINT('Ctrl Pts',(-19.3721499237325,-21.5509644139779,
9.83529244612582));
#213857=CARTESIAN_POINT('Ctrl Pts',(-21.2647362273657,-19.8221870475835,
9.96246825280725));
#213858=CARTESIAN_POINT('Ctrl Pts',(-20.835529117596,-17.2950670749305,
10.0896440594887));
#213859=CARTESIAN_POINT('Ctrl Pts',(-18.4782994780394,-16.2880802201732,
10.2168198661701));
#213860=CARTESIAN_POINT('Ctrl Pts',(-16.3556591968173,-17.7250744218984,
10.3439956728516));
#213861=CARTESIAN_POINT('Ctrl Pts',(-16.414998986037,-20.2876966899422,
10.471171479533));
#213862=CARTESIAN_POINT('Ctrl Pts',(-18.6018782721322,-21.6249001476502,
10.5983472862144));
#213863=CARTESIAN_POINT('Ctrl Pts',(-20.9099710431467,-20.5098836187822,
10.7255230928959));
#213864=CARTESIAN_POINT('Ctrl Pts',(-21.2217454380686,-17.965605562844,
10.8526988995773));
#213865=CARTESIAN_POINT('Ctrl Pts',(-19.2511678004582,-16.3262831804529,
10.9798747062588));
#213866=CARTESIAN_POINT('Ctrl Pts',(-16.8061208049812,-17.0958930096308,
11.1070505129402));
#213867=CARTESIAN_POINT('Ctrl Pts',(-16.1297833132563,-19.5683657994802,
11.2342263196216));
#213868=CARTESIAN_POINT('Ctrl Pts',(-17.8426529957019,-21.4753612242825,
11.361402126303));
#213869=CARTESIAN_POINT('Ctrl Pts',(-20.3732782313567,-21.0673293432663,
11.4885779329845));
#213870=CARTESIAN_POINT('Ctrl Pts',(-21.3999674348234,-18.7186140819493,
11.6157537396659));
#213871=CARTESIAN_POINT('Ctrl Pts',(-19.98079698544,-16.5840159148801,11.7429295463474));
#213872=CARTESIAN_POINT('Ctrl Pts',(-17.4177676868637,-16.6218961722405,
11.8701053530288));
#213873=CARTESIAN_POINT('Ctrl Pts',(-16.0622998409991,-18.7975020690164,
11.9972811597103));
#213874=CARTESIAN_POINT('Ctrl Pts',(-17.1579510666044,-21.1148502282466,
12.1244569663916));
#213875=CARTESIAN_POINT('Ctrl Pts',(-19.6995293679712,-21.4479175446854,
12.2516327730731));
#213876=CARTESIAN_POINT('Ctrl Pts',(-21.3552944017355,-19.4911354279892,
12.3788085797545));
#213877=CARTESIAN_POINT('Ctrl Pts',(-20.6061845177868,-17.0397300186315,
12.505984386436));
#213878=CARTESIAN_POINT('Ctrl Pts',(-18.1394615396447,-16.3427136283187,
12.6331601931174));
#213879=CARTESIAN_POINT('Ctrl Pts',(-16.2181906976602,-18.0395555334466,
12.7603359997988));
#213880=CARTESIAN_POINT('Ctrl Pts',(-16.6050187418368,-20.5735086039467,
12.8875118064803));
#213881=CARTESIAN_POINT('Ctrl Pts',(-18.9450549508987,-21.6198281725,13.0146876131617));
#213882=CARTESIAN_POINT('Ctrl Pts',(-21.0914613420586,-20.2185809768753,
13.1418634198431));
#213883=CARTESIAN_POINT('Ctrl Pts',(-21.0750432724325,-17.6553243478488,
13.2690392265246));
#213884=CARTESIAN_POINT('Ctrl Pts',(-18.9108633018819,-16.2816871489036,
13.396215033206));
#213885=CARTESIAN_POINT('Ctrl Pts',(-16.5844222292293,-17.3578962525319,
13.5233908398874));
#213886=CARTESIAN_POINT('Ctrl Pts',(-16.2300853434153,-19.8965966032252,
13.6505666465689));
#213887=CARTESIAN_POINT('Ctrl Pts',(-18.1729347445473,-21.5686881987366,
13.7777424532503));
#213888=CARTESIAN_POINT('Ctrl Pts',(-20.6305266939199,-20.8401307818932,
13.9049182599318));
#213889=CARTESIAN_POINT('Ctrl Pts',(-21.348173113343,-18.3793305632757,
14.0320940666132));
#213890=CARTESIAN_POINT('Ctrl Pts',(-19.6674779551561,-16.443919008979,
14.1592698732946));
#213891=CARTESIAN_POINT('Ctrl Pts',(-17.1303747112896,-16.8095160948814,
14.2864456799761));
#213892=CARTESIAN_POINT('Ctrl Pts',(-16.0644981376042,-19.140709186182,
14.4136214866575));
#213893=CARTESIAN_POINT('Ctrl Pts',(-17.4477238346954,-21.2987733117736,
14.5407972933389));
#213894=CARTESIAN_POINT('Ctrl Pts',(-20.0110280781508,-21.3038185809918,
14.6679731000203));
#213895=CARTESIAN_POINT('Ctrl Pts',(-21.4027383212044,-19.1512162724734,
14.7951489067018));
#213896=CARTESIAN_POINT('Ctrl Pts',(-20.3460467951339,-16.8158453987172,
14.9223247133832));
#213897=CARTESIAN_POINT('Ctrl Pts',(-17.8104023894363,-16.4402637869306,
15.0495005200647));
#213898=CARTESIAN_POINT('Ctrl Pts',(-16.1221014664979,-18.3690442547039,
15.1766763267461));
#213899=CARTESIAN_POINT('Ctrl Pts',(-16.8300553353419,-20.8326504364724,
15.3038521334275));
#213900=CARTESIAN_POINT('Ctrl Pts',(-19.2847602618764,-21.5708765691077,
15.4310279401089));
#213901=CARTESIAN_POINT('Ctrl Pts',(-21.2341768321763,-19.9064459953984,
15.5582037467904));
#213902=CARTESIAN_POINT('Ctrl Pts',(-20.8898363374295,-17.3663704605105,
15.6853795534718));
#213903=CARTESIAN_POINT('Ctrl Pts',(-18.5676498093848,-16.2810116128359,
15.8125553601533));
#213904=CARTESIAN_POINT('Ctrl Pts',(-16.3980792563722,-17.6461188301484,
15.9397311668347));
#213905=CARTESIAN_POINT('Ctrl Pts',(-16.3715710020456,-20.2092909686735,
16.0669069735161));
#213906=CARTESIAN_POINT('Ctrl Pts',(-18.5124447244619,-21.618976679719,
16.1940827801976));
#213907=CARTESIAN_POINT('Ctrl Pts',(-20.8565816609132,-20.5818768183634,
16.321258586879));
#213908=CARTESIAN_POINT('Ctrl Pts',(-21.2533816657522,-18.0494661377238,
16.4484343935604));
#213909=CARTESIAN_POINT('Ctrl Pts',(-19.338805362725,-16.3450742581534,
16.5756102002418));
#213910=CARTESIAN_POINT('Ctrl Pts',(-16.869357677852,-17.0323749426676,
16.7027860069233));
#213911=CARTESIAN_POINT('Ctrl Pts',(-16.1106035907951,-19.4808124719162,
16.8299618136047));
#213912=CARTESIAN_POINT('Ctrl Pts',(-17.7586528828391,-21.4440973799852,
16.9571376202862));
#213913=CARTESIAN_POINT('Ctrl Pts',(-20.3015226180088,-21.1210376189256,
17.0843134269676));
#213914=CARTESIAN_POINT('Ctrl Pts',(-21.4062876425816,-18.8080204681591,
17.211489233649));
#213915=CARTESIAN_POINT('Ctrl Pts',(-20.0593946159625,-16.6270956014793,
17.3386650403305));
#213916=CARTESIAN_POINT('Ctrl Pts',(-17.4965342924651,-16.5791262206009,
17.4658408470119));
#213917=CARTESIAN_POINT('Ctrl Pts',(-16.0689719498474,-18.7081212551652,
17.5930166536933));
#213918=CARTESIAN_POINT('Ctrl Pts',(-17.0864074329483,-21.0608599012923,
17.7201924603748));
#213919=CARTESIAN_POINT('Ctrl Pts',(-19.6154068351929,-21.4788504785931,
17.8473682670562));
#213920=CARTESIAN_POINT('Ctrl Pts',(-21.3357701724232,-19.5786125758088,
17.9745440737377));
#213921=CARTESIAN_POINT('Ctrl Pts',(-20.6691708605291,-17.1034965266906,
18.1017198804191));
#213922=CARTESIAN_POINT('Ctrl Pts',(-18.2271723943392,-16.3242676832537,
18.2288956871005));
#213923=CARTESIAN_POINT('Ctrl Pts',(-16.2501567990929,-17.9558201449997,
18.3560714937819));
#213924=CARTESIAN_POINT('Ctrl Pts',(-16.5519131759471,-20.5013057937568,
18.4832473004634));
#213925=CARTESIAN_POINT('Ctrl Pts',(-18.8555987783568,-21.6253995376139,
18.6104231071448));
#213926=CARTESIAN_POINT('Ctrl Pts',(-21.0477250487613,-20.2968151353882,
18.7375989138263));
#213927=CARTESIAN_POINT('Ctrl Pts',(-21.1171521931581,-17.7344463154909,
18.8647747205077));
#213928=CARTESIAN_POINT('Ctrl Pts',(-19.000185114941,-16.2891074304433,
18.9919505271891));
#213929=CARTESIAN_POINT('Ctrl Pts',(-16.6390097160369,-17.2868072017201,
19.1191263338706));
#213930=CARTESIAN_POINT('Ctrl Pts',(-16.1998578710576,-19.8122180089903,
19.246302140552));
#213931=CARTESIAN_POINT('Ctrl Pts',(-18.0856241463476,-21.5484321897643,
19.3734779472334));
#213932=CARTESIAN_POINT('Ctrl Pts',(-20.566235017753,-20.9025809783934,
19.5006537539149));
#213933=CARTESIAN_POINT('Ctrl Pts',(-21.3658839949308,-18.4671928068505,
19.6278295605963));
#213934=CARTESIAN_POINT('Ctrl Pts',(-19.7509427344116,-16.4765851044279,
19.7550053672777));
#213935=CARTESIAN_POINT('Ctrl Pts',(-17.2030196827703,-16.757017004315,
19.8821811739592));
#213936=CARTESIAN_POINT('Ctrl Pts',(-16.0596759541972,-19.0512094179914,
20.0093569806406));
#213937=CARTESIAN_POINT('Ctrl Pts',(-17.3698587327168,-21.2543836348827,
20.136532787322));
#213938=CARTESIAN_POINT('Ctrl Pts',(-19.9315561044895,-21.3452632166212,
20.2637085940035));
#213939=CARTESIAN_POINT('Ctrl Pts',(-21.394570756024,-19.2404734037209,
20.3908844006849));
#213940=CARTESIAN_POINT('Ctrl Pts',(-20.4166755682946,-16.8710250976204,
20.5180602073664));
#213941=CARTESIAN_POINT('Ctrl Pts',(-17.8950324982703,-16.4107460543773,
20.6452360140478));
#213942=CARTESIAN_POINT('Ctrl Pts',(-16.1430851969531,-18.281902167926,
20.7724118207292));
#213943=CARTESIAN_POINT('Ctrl Pts',(-16.7681507463741,-20.7678461146898,
20.8995876274106));
#213944=CARTESIAN_POINT('Ctrl Pts',(-19.1967429963892,-21.58783570276,21.0267634340921));
#213945=CARTESIAN_POINT('Ctrl Pts',(-21.2008319023016,-19.989664067993,
21.1539392407735));
#213946=CARTESIAN_POINT('Ctrl Pts',(-20.9416889151052,-17.4393951699213,
21.2811150474549));
#213947=CARTESIAN_POINT('Ctrl Pts',(-18.6572569499448,-16.2770494137143,
21.4082908541364));
#213948=CARTESIAN_POINT('Ctrl Pts',(-16.4429842219372,-17.568415375407,
21.5354666608178));
#213949=CARTESIAN_POINT('Ctrl Pts',(-16.3310537276957,-20.1298849908433,
21.6626424674993));
#213950=CARTESIAN_POINT('Ctrl Pts',(-18.4227563856442,-21.6092689274519,
21.7898182741806));
#213951=CARTESIAN_POINT('Ctrl Pts',(-20.8017892824853,-20.6535945073695,
21.9169940808621));
#213952=CARTESIAN_POINT('Ctrl Pts',(-21.2802305760296,-18.1311084332283,
22.0441698875435));
#213953=CARTESIAN_POINT('Ctrl Pts',(-20.0469417623915,-16.9604786618337,
22.1289537586645));
#213954=CARTESIAN_POINT('Ctrl Pts',(-19.319022416489,-16.7656980906223,
22.171345694225));
#213955=CARTESIAN_POINT('Ctrl Pts',(-16.8880688553878,-17.3975534516058,
-0.171094837061568));
#213956=CARTESIAN_POINT('Ctrl Pts',(-16.3702697975385,-18.0124051053735,
-0.12868424499791));
#213957=CARTESIAN_POINT('Ctrl Pts',(-16.0068254820486,-19.7893209524259,
-0.043881717373774));
#213958=CARTESIAN_POINT('Ctrl Pts',(-17.9658932450075,-21.7021720009294,
0.0833127458108395));
#213959=CARTESIAN_POINT('Ctrl Pts',(-20.6289595651085,-21.0844926888652,
0.210488552492275));
#213960=CARTESIAN_POINT('Ctrl Pts',(-21.5536820848537,-18.5139386369225,
0.337664359173709));
#213961=CARTESIAN_POINT('Ctrl Pts',(-19.8914410613435,-16.3434494886539,
0.464840165855143));
#213962=CARTESIAN_POINT('Ctrl Pts',(-17.1673608327897,-16.567091225276,
0.592015972536577));
#213963=CARTESIAN_POINT('Ctrl Pts',(-15.8805535113812,-18.9782470561293,
0.719191779218012));
#213964=CARTESIAN_POINT('Ctrl Pts',(-17.2116172834215,-21.365578009315,
0.846367585899446));
#213965=CARTESIAN_POINT('Ctrl Pts',(-19.939366976384,-21.5384685112341,
0.97354339258088));
#213966=CARTESIAN_POINT('Ctrl Pts',(-21.5612702568039,-19.3385034208011,
1.10071919926231));
#213967=CARTESIAN_POINT('Ctrl Pts',(-20.5893270128691,-16.7839097584284,
1.22789500594375));
#213968=CARTESIAN_POINT('Ctrl Pts',(-17.9152371905106,-16.2184228400477,
1.35507081262518));
#213969=CARTESIAN_POINT('Ctrl Pts',(-15.9923110118271,-18.1608136920126,
1.48224661930662));
#213970=CARTESIAN_POINT('Ctrl Pts',(-16.5847145272265,-20.8290738621089,
1.60942242598805));
#213971=CARTESIAN_POINT('Ctrl Pts',(-19.1489539521699,-21.7752326797234,
1.73659823266948));
#213972=CARTESIAN_POINT('Ctrl Pts',(-21.3324989390857,-20.1312520866371,
1.86377403935092));
#213973=CARTESIAN_POINT('Ctrl Pts',(-21.1320824002478,-17.4053801994873,
1.99094984603235));
#213974=CARTESIAN_POINT('Ctrl Pts',(-18.731574116624,-16.0984363471145,
2.11812565271379));
#213975=CARTESIAN_POINT('Ctrl Pts',(-16.3332914223019,-17.4094598463232,
2.24530145939522));
#213976=CARTESIAN_POINT('Ctrl Pts',(-16.1375098474575,-20.1356682931634,
2.37247726607666));
#213977=CARTESIAN_POINT('Ctrl Pts',(-18.3238468290274,-21.7759344971771,
2.49965307275809));
#213978=CARTESIAN_POINT('Ctrl Pts',(-20.8864738891242,-20.8254160994288,
2.62682887943953));
#213979=CARTESIAN_POINT('Ctrl Pts',(-21.4743397529562,-18.1561546941444,
2.75400468612096));
#213980=CARTESIAN_POINT('Ctrl Pts',(-19.5481139784241,-16.2170319683244,
2.88118049280239));
#213981=CARTESIAN_POINT('Ctrl Pts',(-16.8749891581411,-16.7870726566358,
3.00835629948383));
#213982=CARTESIAN_POINT('Ctrl Pts',(-15.9073914021204,-19.3432998138438,
3.13553210616526));
#213983=CARTESIAN_POINT('Ctrl Pts',(-17.533031595496,-21.5405336776668,
3.2627079128467));
#213984=CARTESIAN_POINT('Ctrl Pts',(-20.2604857595204,-21.3629485552631,
3.38988371952813));
#213985=CARTESIAN_POINT('Ctrl Pts',(-21.5874839835647,-18.9734677734828,
3.51705952620957));
#213986=CARTESIAN_POINT('Ctrl Pts',(-20.2965877598843,-16.5642916421105,
3.644235332891));
#213987=CARTESIAN_POINT('Ctrl Pts',(-17.5721142516412,-16.3456897311358,
3.77141113957244));
#213988=CARTESIAN_POINT('Ctrl Pts',(-15.9135988027563,-18.5182157260222,
3.89858694625387));
#213989=CARTESIAN_POINT('Ctrl Pts',(-16.8426263985009,-21.0887118685754,
4.0257627529353));
#213990=CARTESIAN_POINT('Ctrl Pts',(-19.5068718817363,-21.6989074910159,
4.15293855961674));
#213991=CARTESIAN_POINT('Ctrl Pts',(-21.4620553833173,-19.7889859827511,
4.28011436629817));
#213992=CARTESIAN_POINT('Ctrl Pts',(-20.9144173929179,-17.1111817845236,
4.40729017297961));
#213993=CARTESIAN_POINT('Ctrl Pts',(-18.3663817764822,-16.1222140449305,
4.53446597966104));
#213994=CARTESIAN_POINT('Ctrl Pts',(-16.1556130631639,-17.7293992827899,
4.66164178634248));
#213995=CARTESIAN_POINT('Ctrl Pts',(-16.310354331651,-20.4582447955307,
4.78881759302391));
#213996=CARTESIAN_POINT('Ctrl Pts',(-18.6886400724331,-21.8052041964678,
4.91599339970535));
#213997=CARTESIAN_POINT('Ctrl Pts',(-21.1085407314031,-20.5345258369701,
5.04316920638678));
#213998=CARTESIAN_POINT('Ctrl Pts',(-21.34994764993,-17.8119782446832,5.17034501306821));
#213999=CARTESIAN_POINT('Ctrl Pts',(-19.1913849636685,-16.1353298551694,
5.29752081974965));
#214000=CARTESIAN_POINT('Ctrl Pts',(-16.6131999617537,-17.0428015012722,
5.42469662643108));
#214001=CARTESIAN_POINT('Ctrl Pts',(-15.9807173632341,-19.7018442717348,
5.55187243311253));
#214002=CARTESIAN_POINT('Ctrl Pts',(-17.8742006959542,-21.672951463465,
5.67904823979394));
#214003=CARTESIAN_POINT('Ctrl Pts',(-20.556496524973,-21.1477545687602,
5.80622404647539));
#214004=CARTESIAN_POINT('Ctrl Pts',(-21.5667649092207,-18.6080891411163,
5.93339985315682));
#214005=CARTESIAN_POINT('Ctrl Pts',(-19.9781473104775,-16.3839405809831,
6.06057565983826));
#214006=CARTESIAN_POINT('Ctrl Pts',(-17.2481017748621,-16.5158271460542,
6.18775146651969));
#214007=CARTESIAN_POINT('Ctrl Pts',(-15.8812756355658,-18.8827510986805,
6.31492727320112));
#214008=CARTESIAN_POINT('Ctrl Pts',(-17.1316470405952,-21.3132066201958,
6.44210307988256));
#214009=CARTESIAN_POINT('Ctrl Pts',(-19.8520778326375,-21.5774016206925,
6.569278886564));
#214010=CARTESIAN_POINT('Ctrl Pts',(-21.5467416089716,-19.4329535850057,
6.69645469324542));
#214011=CARTESIAN_POINT('Ctrl Pts',(-20.6608895375072,-16.8472604864224,
6.82363049992686));
#214012=CARTESIAN_POINT('Ctrl Pts',(-18.0072359116326,-16.1925352566794,
6.95080630660829));
#214013=CARTESIAN_POINT('Ctrl Pts',(-16.0203432287685,-18.0694476572352,
7.07798211328973));
#214014=CARTESIAN_POINT('Ctrl Pts',(-16.5230622049748,-20.7560470549016,
7.20515791997116));
#214015=CARTESIAN_POINT('Ctrl Pts',(-19.0541793818409,-21.7875452514841,
7.3323337266526));
#214016=CARTESIAN_POINT('Ctrl Pts',(-21.2915518484416,-20.2176066736166,
7.45950953333402));
#214017=CARTESIAN_POINT('Ctrl Pts',(-21.1825292336674,-17.4865525251151,
7.58668534001548));
#214018=CARTESIAN_POINT('Ctrl Pts',(-18.8271330198668,-16.0999554788923,
7.71386114669689));
#214019=CARTESIAN_POINT('Ctrl Pts',(-16.3862930408257,-17.3299322629389,
7.84103695337835));
#214020=CARTESIAN_POINT('Ctrl Pts',(-16.0993284816994,-20.0480555188611,
7.96821276005976));
#214021=CARTESIAN_POINT('Ctrl Pts',(-18.2295115144572,-21.760615865106,
8.09538856674121));
#214022=CARTESIAN_POINT('Ctrl Pts',(-20.8225314206137,-20.8964454774766,
8.22256437342263));
#214023=CARTESIAN_POINT('Ctrl Pts',(-21.4994533772365,-18.2483670501596,
8.34974018010408));
#214024=CARTESIAN_POINT('Ctrl Pts',(-19.6392435036391,-16.245828181935,
8.4769159867855));
#214025=CARTESIAN_POINT('Ctrl Pts',(-16.9485289012012,-16.7260339928192,
8.60409179346695));
#214026=CARTESIAN_POINT('Ctrl Pts',(-15.8958732130767,-19.2484254562599,
8.73126760014836));
#214027=CARTESIAN_POINT('Ctrl Pts',(-17.4470226979395,-21.4988649618209,
8.85844340682981));
#214028=CARTESIAN_POINT('Ctrl Pts',(-20.1788939786226,-21.4127139411785,
8.98561921351124));
#214029=CARTESIAN_POINT('Ctrl Pts',(-21.5851647141539,-19.0690106086366,
9.11279502019268));
#214030=CARTESIAN_POINT('Ctrl Pts',(-20.3756687876888,-16.617957305168,
9.23997082687412));
#214031=CARTESIAN_POINT('Ctrl Pts',(-17.6600436419756,-16.3082433071803,
9.36714663355554));
#214032=CARTESIAN_POINT('Ctrl Pts',(-15.9297067975006,-18.4240119848083,
9.49432244023699));
#214033=CARTESIAN_POINT('Ctrl Pts',(-16.772134912253,-21.0241768957426,
9.62149824691841));
#214034=CARTESIAN_POINT('Ctrl Pts',(-19.4144524779331,-21.7232481186362,
9.74867405359986));
#214035=CARTESIAN_POINT('Ctrl Pts',(-21.4324971287534,-19.8798711957376,
9.87584986028127));
#214036=CARTESIAN_POINT('Ctrl Pts',(-20.9748381515633,-17.1852300409311,
10.0030256669627));
#214037=CARTESIAN_POINT('Ctrl Pts',(-18.461349252415,-16.1114906654595,
10.1302014736441));
#214038=CARTESIAN_POINT('Ctrl Pts',(-16.1980004915621,-17.6437423025364,
10.2573772803256));
#214039=CARTESIAN_POINT('Ctrl Pts',(-16.2612738778198,-20.3762391774058,
10.384553087007));
#214040=CARTESIAN_POINT('Ctrl Pts',(-18.5931200064859,-21.8020850052583,
10.5117288936884));
#214041=CARTESIAN_POINT('Ctrl Pts',(-21.0542147852026,-20.6131547370118,
10.6389047003698));
#214042=CARTESIAN_POINT('Ctrl Pts',(-21.3866565072667,-17.900218100448,
10.7660805070513));
#214043=CARTESIAN_POINT('Ctrl Pts',(-19.2854505263445,-16.152226075776,
10.8932563137327));
#214044=CARTESIAN_POINT('Ctrl Pts',(-16.678322914381,-16.9728528530119,
11.0204321204142));
#214045=CARTESIAN_POINT('Ctrl Pts',(-15.9571514387634,-19.6092242978837,
11.1476079270956));
#214046=CARTESIAN_POINT('Ctrl Pts',(-17.7835661674212,-21.6426332413875,
11.274783733777));
#214047=CARTESIAN_POINT('Ctrl Pts',(-20.4819449468934,-21.2075531854514,
11.4019595404585));
#214048=CARTESIAN_POINT('Ctrl Pts',(-21.5766927272896,-18.7031430772827,
11.5291353471399));
#214049=CARTESIAN_POINT('Ctrl Pts',(-20.0634463678067,-16.4270437499047,
11.6563111538213));
#214050=CARTESIAN_POINT('Ctrl Pts',(-17.3305154806086,-16.4674350655298,
11.7834869605028));
#214051=CARTESIAN_POINT('Ctrl Pts',(-15.8851945298786,-18.78726049904,11.9106627671842));
#214052=CARTESIAN_POINT('Ctrl Pts',(-17.0534757811762,-21.2582241997943,
12.0378385738656));
#214053=CARTESIAN_POINT('Ctrl Pts',(-19.7635336981482,-21.6133703376545,
12.1650143805471));
#214054=CARTESIAN_POINT('Ctrl Pts',(-21.5290583471371,-19.526874373989,
12.2921901872285));
#214055=CARTESIAN_POINT('Ctrl Pts',(-20.7302904435136,-16.9129668529163,
12.4193659939099));
#214056=CARTESIAN_POINT('Ctrl Pts',(-18.1000499617251,-16.1697456876228,
12.5465418005913));
#214057=CARTESIAN_POINT('Ctrl Pts',(-16.0514192926768,-17.9790701677574,
12.6737176072728));
#214058=CARTESIAN_POINT('Ctrl Pts',(-16.4638899228612,-20.6809973821388,
12.8008934139542));
#214059=CARTESIAN_POINT('Ctrl Pts',(-18.9590456498985,-21.7966768120881,
12.9280692206357));
#214060=CARTESIAN_POINT('Ctrl Pts',(-21.2477359610623,-20.3025418275019,
13.0552450273171));
#214061=CARTESIAN_POINT('Ctrl Pts',(-21.2302295480009,-17.569368540262,
13.1824208339985));
#214062=CARTESIAN_POINT('Ctrl Pts',(-18.9225874581277,-16.1046738015453,
13.30959664068));
#214063=CARTESIAN_POINT('Ctrl Pts',(-16.44192808048,-17.2522241249159,13.4367724473614));
#214064=CARTESIAN_POINT('Ctrl Pts',(-16.0641024269644,-19.9592133136872,
13.5639482540428));
#214065=CARTESIAN_POINT('Ctrl Pts',(-18.1357420841767,-21.7421468018591,
13.6911240607243));
#214066=CARTESIAN_POINT('Ctrl Pts',(-20.7562462470829,-20.9652937753664,
13.8182998674057));
#214067=CARTESIAN_POINT('Ctrl Pts',(-21.521464993048,-18.3413686690794,
13.9454756740872));
#214068=CARTESIAN_POINT('Ctrl Pts',(-19.7293576174809,-16.2776599088574,
14.0726514807686));
#214069=CARTESIAN_POINT('Ctrl Pts',(-17.0240714067361,-16.6674921939926,
14.19982728745));
#214070=CARTESIAN_POINT('Ctrl Pts',(-15.8875385501732,-19.1532185985939,
14.3270030941314));
#214071=CARTESIAN_POINT('Ctrl Pts',(-17.3624574025039,-21.4543394280201,
14.4541789008129));
#214072=CARTESIAN_POINT('Ctrl Pts',(-20.0956814605031,-21.4597191449386,
14.5813547074943));
#214073=CARTESIAN_POINT('Ctrl Pts',(-21.5796472939737,-19.1644221929799,
14.7085305141757));
#214074=CARTESIAN_POINT('Ctrl Pts',(-20.4529083560135,-16.6742410633702,
14.8357063208572));
#214075=CARTESIAN_POINT('Ctrl Pts',(-17.7491776888957,-16.2737623844548,
14.9628821275386));
#214076=CARTESIAN_POINT('Ctrl Pts',(-15.9489603672498,-18.3304004876284,
15.0900579342201));
#214077=CARTESIAN_POINT('Ctrl Pts',(-16.7038440495977,-20.9573175625861,
15.2172337409015));
#214078=CARTESIAN_POINT('Ctrl Pts',(-19.3212698107507,-21.7444802379159,
15.3444095475829));
#214079=CARTESIAN_POINT('Ctrl Pts',(-21.3999119706151,-19.9697156158284,
15.4715853542643));
#214080=CARTESIAN_POINT('Ctrl Pts',(-21.032745362598,-17.2612600827733,
15.5987611609458));
#214081=CARTESIAN_POINT('Ctrl Pts',(-18.5566225606254,-16.1039534846195,
15.7259369676272));
#214082=CARTESIAN_POINT('Ctrl Pts',(-16.2432325499933,-17.5595527946246,
15.8531127743086));
#214083=CARTESIAN_POINT('Ctrl Pts',(-16.2149670802795,-20.2926359905412,
15.9802885809901));
#214084=CARTESIAN_POINT('Ctrl Pts',(-18.4977579655933,-21.7957688743899,
16.1074643876715));
#214085=CARTESIAN_POINT('Ctrl Pts',(-20.997286254641,-20.6899203201883,
16.234640194353));
#214086=CARTESIAN_POINT('Ctrl Pts',(-21.4203898804431,-17.9896377397141,
16.3618160010344));
#214087=CARTESIAN_POINT('Ctrl Pts',(-19.378897527099,-16.1722628021139,
16.4889918077158));
#214088=CARTESIAN_POINT('Ctrl Pts',(-16.7457517194962,-16.9051242136259,
16.6161676143973));
#214089=CARTESIAN_POINT('Ctrl Pts',(-15.9367003046499,-19.5158671156972,
16.7433434210787));
#214090=CARTESIAN_POINT('Ctrl Pts',(-17.6939977402874,-21.6092969366562,
16.8705192277601));
#214091=CARTESIAN_POINT('Ctrl Pts',(-20.4054326993911,-21.2648217486819,
16.9976950344416));
#214092=CARTESIAN_POINT('Ctrl Pts',(-21.5834318976165,-18.798476156199,
17.124870841123));
#214093=CARTESIAN_POINT('Ctrl Pts',(-20.147254185468,-16.4729791616393,
17.2520466478045));
#214094=CARTESIAN_POINT('Ctrl Pts',(-17.4145034745997,-16.4218299208892,
17.3792224544858));
#214095=CARTESIAN_POINT('Ctrl Pts',(-15.8923089285959,-18.691954687658,
17.5063982611673));
#214096=CARTESIAN_POINT('Ctrl Pts',(-16.9771895653652,-21.2006548882669,
17.6335740678487));
#214097=CARTESIAN_POINT('Ctrl Pts',(-19.6738347359605,-21.646353796156,
17.7607498745302));
#214098=CARTESIAN_POINT('Ctrl Pts',(-21.5082398690315,-19.6201503265241,
17.8879256812116));
#214099=CARTESIAN_POINT('Ctrl Pts',(-20.7974521110171,-16.980960402401,
18.015101487893));
#214100=CARTESIAN_POINT('Ctrl Pts',(-18.1935751134159,-16.1500769725442,
18.1422772945745));
#214101=CARTESIAN_POINT('Ctrl Pts',(-16.0855044067243,-17.8897840134535,
18.2694531012559));
#214102=CARTESIAN_POINT('Ctrl Pts',(-16.407264022649,-20.6040082933991,
18.3966289079374));
#214103=CARTESIAN_POINT('Ctrl Pts',(-18.8636594843459,-21.8026174994662,
18.5238047146188));
#214104=CARTESIAN_POINT('Ctrl Pts',(-21.2011004165875,-20.3859620788242,
18.6509805213002));
#214105=CARTESIAN_POINT('Ctrl Pts',(-21.275129842407,-17.6537354530185,
18.7781563279817));
#214106=CARTESIAN_POINT('Ctrl Pts',(-19.0178303575923,-16.1125859688478,
18.9053321346631));
#214107=CARTESIAN_POINT('Ctrl Pts',(-16.500134137209,-17.1764226259579,
19.0325079413445));
#214108=CARTESIAN_POINT('Ctrl Pts',(-16.031871194612,-19.8692413158911,
19.1596837480259));
#214109=CARTESIAN_POINT('Ctrl Pts',(-18.0426437217303,-21.7205480348836,
19.2868595547074));
#214110=CARTESIAN_POINT('Ctrl Pts',(-20.6876927164292,-21.0318837558328,
19.4140353613888));
#214111=CARTESIAN_POINT('Ctrl Pts',(-21.5403499177572,-18.4350552451234,
19.5412111680702));
#214112=CARTESIAN_POINT('Ctrl Pts',(-19.8183552240814,-16.3124914190809,
19.6683869747517));
#214113=CARTESIAN_POINT('Ctrl Pts',(-17.1015319673585,-16.6115129719686,
19.7955627814331));
#214114=CARTESIAN_POINT('Ctrl Pts',(-15.8823967072827,-19.0577859474646,
19.9227385881146));
#214115=CARTESIAN_POINT('Ctrl Pts',(-17.2794306722399,-21.4070071875673,
20.049914394796));
#214116=CARTESIAN_POINT('Ctrl Pts',(-20.0109413400502,-21.5039111192106,
20.1770902014775));
#214117=CARTESIAN_POINT('Ctrl Pts',(-21.5709383060712,-19.2595961229167,
20.3042660081589));
#214118=CARTESIAN_POINT('Ctrl Pts',(-20.5282190658065,-16.7330785895595,
20.4314418148403));
#214119=CARTESIAN_POINT('Ctrl Pts',(-17.8394178740343,-16.242287940109,
20.5586176215217));
#214120=CARTESIAN_POINT('Ctrl Pts',(-15.9713350959043,-18.2374818071192,
20.6857934282033));
#214121=CARTESIAN_POINT('Ctrl Pts',(-16.6378358446413,-20.8882174033637,
20.8129692348846));
#214122=CARTESIAN_POINT('Ctrl Pts',(-19.2274179364899,-21.762563581795,
20.9401450415661));
#214123=CARTESIAN_POINT('Ctrl Pts',(-21.3643566264617,-20.0584501617399,
21.0673208482475));
#214124=CARTESIAN_POINT('Ctrl Pts',(-21.0880352148013,-17.3391255539126,
21.1944966549289));
#214125=CARTESIAN_POINT('Ctrl Pts',(-18.6521697017704,-16.099728633828,
21.3216724616103));
#214126=CARTESIAN_POINT('Ctrl Pts',(-16.2911142372801,-17.4766984270906,
21.4488482682918));
#214127=CARTESIAN_POINT('Ctrl Pts',(-16.171763941479,-20.2079662407414,
21.5760240749733));
#214128=CARTESIAN_POINT('Ctrl Pts',(-18.4021242436095,-21.7854176013747,
21.7031998816546));
#214129=CARTESIAN_POINT('Ctrl Pts',(-20.9388617241559,-20.7663921293681,
21.8303756883361));
#214130=CARTESIAN_POINT('Ctrl Pts',(-21.4490185879752,-18.0766920512704,
21.9575514950176));
#214131=CARTESIAN_POINT('Ctrl Pts',(-20.1339758401221,-16.8284619738791,
22.0423353661385));
#214132=CARTESIAN_POINT('Ctrl Pts',(-19.3578031818887,-16.6207695219882,
22.0847273016989));
#214133=CARTESIAN_POINT('Ctrl Pts',(-16.7733105073354,-17.3009161969877,
-0.257713229587528));
#214134=CARTESIAN_POINT('Ctrl Pts',(-16.2233207772202,-17.9539921151271,
-0.21530263752387));
#214135=CARTESIAN_POINT('Ctrl Pts',(-15.8372817569514,-19.8413757484949,
-0.130500109899735));
#214136=CARTESIAN_POINT('Ctrl Pts',(-17.9181413759371,-21.8731454397858,
-0.00330564671512121));
#214137=CARTESIAN_POINT('Ctrl Pts',(-20.7467659253037,-21.217066072722,
0.123870159966314));
#214138=CARTESIAN_POINT('Ctrl Pts',(-21.7289768454601,-18.4867051192915,
0.251045966647748));
#214139=CARTESIAN_POINT('Ctrl Pts',(-19.9633971711666,-16.1812804129726,
0.378221773329183));
#214140=CARTESIAN_POINT('Ctrl Pts',(-17.0699655841381,-16.4188255697332,
0.505397580010616));
#214141=CARTESIAN_POINT('Ctrl Pts',(-15.703159676164,-18.9798787902335,
0.632573386692052));
#214142=CARTESIAN_POINT('Ctrl Pts',(-17.1169733817962,-21.5156259816095,
0.759749193373485));
#214143=CARTESIAN_POINT('Ctrl Pts',(-20.0143025574919,-21.6992647871434,
0.88692500005492));
#214144=CARTESIAN_POINT('Ctrl Pts',(-21.7370367609421,-19.362531670293,
1.01410080673636));
#214145=CARTESIAN_POINT('Ctrl Pts',(-20.7046694858076,-16.6491233362602,
1.14127661341778));
#214146=CARTESIAN_POINT('Ctrl Pts',(-17.8643361221052,-16.0484810737661,
1.26845242009923));
#214147=CARTESIAN_POINT('Ctrl Pts',(-15.8218649472086,-18.1116270070318,
1.39562822678066));
#214148=CARTESIAN_POINT('Ctrl Pts',(-16.4510971650251,-20.9457682990692,
1.52280403346208));
#214149=CARTESIAN_POINT('Ctrl Pts',(-19.1747509220124,-21.9507481746746,
1.64997984014353));
#214150=CARTESIAN_POINT('Ctrl Pts',(-21.4940431258966,-20.2045641501962,
1.77715564682495));
#214151=CARTESIAN_POINT('Ctrl Pts',(-21.2811670373152,-17.3092295202543,
1.9043314535064));
#214152=CARTESIAN_POINT('Ctrl Pts',(-18.7314233036483,-15.9210352279973,
2.03150726018784));
#214153=CARTESIAN_POINT('Ctrl Pts',(-16.1840435203226,-17.3135627916812,
2.15868306686927));
#214154=CARTESIAN_POINT('Ctrl Pts',(-15.9760905434333,-20.2092549046476,
2.2858588735507));
#214155=CARTESIAN_POINT('Ctrl Pts',(-18.2983483154525,-21.9514936229061,
2.41303468023214));
#214156=CARTESIAN_POINT('Ctrl Pts',(-21.020289469658,-20.9418831396066,
2.54021048691357));
#214157=CARTESIAN_POINT('Ctrl Pts',(-21.644701937954,-18.1066783673205,
2.667386293595));
#214158=CARTESIAN_POINT('Ctrl Pts',(-19.598726037039,-16.0470037339522,
2.79456210027644));
#214159=CARTESIAN_POINT('Ctrl Pts',(-16.7594176679228,-16.6524828663812,
2.92173790695787));
#214160=CARTESIAN_POINT('Ctrl Pts',(-15.7316660321737,-19.3676262467993,
3.04891371363931));
#214161=CARTESIAN_POINT('Ctrl Pts',(-17.4583694659978,-21.7014583414031,
3.17608952032074));
#214162=CARTESIAN_POINT('Ctrl Pts',(-20.3553847402323,-21.512833058945,
3.30326532700218));
#214163=CARTESIAN_POINT('Ctrl Pts',(-21.7648801497778,-18.9748023878472,
3.43044113368361));
#214164=CARTESIAN_POINT('Ctrl Pts',(-20.3937311395464,-16.4158519413221,
3.55761694036505));
#214165=CARTESIAN_POINT('Ctrl Pts',(-17.4998818233102,-16.1836599274567,
3.68479274704648));
#214166=CARTESIAN_POINT('Ctrl Pts',(-15.7382593361759,-18.4912481076264,
3.81196855372791));
#214167=CARTESIAN_POINT('Ctrl Pts',(-16.7250429714639,-21.2215475515407,
3.93914436040935));
#214168=CARTESIAN_POINT('Ctrl Pts',(-19.5549199904986,-21.8696779809346,
4.06632016709078));
#214169=CARTESIAN_POINT('Ctrl Pts',(-21.6316538702915,-19.8410199543343,
4.19349597377222));
#214170=CARTESIAN_POINT('Ctrl Pts',(-21.0499701727744,-16.9967412984365,
4.32067178045365));
#214171=CARTESIAN_POINT('Ctrl Pts',(-18.3435275870569,-15.9462911441802,
4.44784758713509));
#214172=CARTESIAN_POINT('Ctrl Pts',(-15.9953192047637,-17.6533923098082,
4.57502339381652));
#214173=CARTESIAN_POINT('Ctrl Pts',(-16.159680470399,-20.5518854305035,
4.70219920049796));
#214174=CARTESIAN_POINT('Ctrl Pts',(-18.6858201241535,-21.9825829688008,
4.82937500717939));
#214175=CARTESIAN_POINT('Ctrl Pts',(-21.2561618236167,-20.632908732416,
4.95655081386082));
#214176=CARTESIAN_POINT('Ctrl Pts',(-21.5125765929291,-17.7411050630016,
5.08372662054225));
#214177=CARTESIAN_POINT('Ctrl Pts',(-19.219819796142,-15.9602223416674,
5.21090242722368));
#214178=CARTESIAN_POINT('Ctrl Pts',(-16.4813534897718,-16.9241099311898,
5.33807823390512));
#214179=CARTESIAN_POINT('Ctrl Pts',(-15.8095505415254,-19.748460793793,
5.46525404058656));
#214180=CARTESIAN_POINT('Ctrl Pts',(-17.8207484596252,-21.8421083120231,
5.59242984726799));
#214181=CARTESIAN_POINT('Ctrl Pts',(-20.6697979832357,-21.2842608343242,
5.71960565394943));
#214182=CARTESIAN_POINT('Ctrl Pts',(-21.7428730064005,-18.5867087975656,
5.84678146063087));
#214183=CARTESIAN_POINT('Ctrl Pts',(-20.0554937979133,-16.2242887665116,
5.9739572673123));
#214184=CARTESIAN_POINT('Ctrl Pts',(-17.1557260509959,-16.3643744913304,
6.10113307399374));
#214185=CARTESIAN_POINT('Ctrl Pts',(-15.7039266935608,-18.8784460142016,
6.22830888067516));
#214186=CARTESIAN_POINT('Ctrl Pts',(-17.0320315272241,-21.4599987537674,
6.3554846873566));
#214187=CARTESIAN_POINT('Ctrl Pts',(-19.9215867985823,-21.7406183007101,
6.48266049403803));
#214188=CARTESIAN_POINT('Ctrl Pts',(-21.7216048921908,-19.4628536379228,
6.60983630071947));
#214189=CARTESIAN_POINT('Ctrl Pts',(-20.7806809288866,-16.7164124694941,
6.73701210740091));
#214190=CARTESIAN_POINT('Ctrl Pts',(-17.9620542446739,-16.0209841040936,
6.86418791408233));
#214191=CARTESIAN_POINT('Ctrl Pts',(-15.8516398786157,-18.0145809038241,
6.99136372076378));
#214192=CARTESIAN_POINT('Ctrl Pts',(-16.3856120244824,-20.868201541505,
7.11853952744521));
#214193=CARTESIAN_POINT('Ctrl Pts',(-19.0740843804904,-21.9638261977359,
7.24571533412664));
#214194=CARTESIAN_POINT('Ctrl Pts',(-21.4505504254156,-20.2962872525602,
7.37289114080807));
#214195=CARTESIAN_POINT('Ctrl Pts',(-21.3347500631569,-17.3954481890373,
7.50006694748951));
#214196=CARTESIAN_POINT('Ctrl Pts',(-18.8329229387055,-15.9226488015715,
7.62724275417095));
#214197=CARTESIAN_POINT('Ctrl Pts',(-16.2403401578418,-17.2290911159235,
7.75441856085238));
#214198=CARTESIAN_POINT('Ctrl Pts',(-15.9355355081732,-20.1161953956302,
7.8815943675338));
#214199=CARTESIAN_POINT('Ctrl Pts',(-18.1981483374604,-21.9352226579616,
8.00877017421523));
#214200=CARTESIAN_POINT('Ctrl Pts',(-20.9523718084226,-21.0173282912935,
8.13594598089668));
#214201=CARTESIAN_POINT('Ctrl Pts',(-21.6713768328398,-18.2046234060944,
8.26312178757812));
#214202=CARTESIAN_POINT('Ctrl Pts',(-19.6955209272938,-16.0775901583807,
8.39029759425955));
#214203=CARTESIAN_POINT('Ctrl Pts',(-16.837529249675,-16.5876495343575,
8.51747340094099));
#214204=CARTESIAN_POINT('Ctrl Pts',(-15.7194317772296,-19.2668537144213,
8.64464920762241));
#214205=CARTESIAN_POINT('Ctrl Pts',(-17.3670135439705,-21.657199153529,
8.77182501430386));
#214206=CARTESIAN_POINT('Ctrl Pts',(-20.2687205393704,-21.5656922728693,
8.89900082098528));
#214207=CARTESIAN_POINT('Ctrl Pts',(-21.7624166953973,-19.07628495589,9.02617662766673));
#214208=CARTESIAN_POINT('Ctrl Pts',(-20.4777284981358,-16.4728539058758,
9.15335243434816));
#214209=CARTESIAN_POINT('Ctrl Pts',(-17.5932776318311,-16.1438855240604,
9.28052824102959));
#214210=CARTESIAN_POINT('Ctrl Pts',(-15.7553687371063,-18.3911878826788,
9.40770404771103));
#214211=CARTESIAN_POINT('Ctrl Pts',(-16.6501691513803,-21.1530005510137,
9.53487985439246));
#214212=CARTESIAN_POINT('Ctrl Pts',(-19.4567550321338,-21.8955318232944,
9.6620556610739));
#214213=CARTESIAN_POINT('Ctrl Pts',(-21.6002580301411,-19.9375553438918,
9.78923146775533));
#214214=CARTESIAN_POINT('Ctrl Pts',(-21.1141471855306,-17.0753930069318,
9.91640727443676));
#214215=CARTESIAN_POINT('Ctrl Pts',(-18.4443990267908,-15.9349011107459,
10.0435830811182));
#214216=CARTESIAN_POINT('Ctrl Pts',(-16.0403417863069,-17.5624101831744,
10.1707588877996));
#214217=CARTESIAN_POINT('Ctrl Pts',(-16.1075487696024,-20.4647816648694,
10.297934694481));
#214218=CARTESIAN_POINT('Ctrl Pts',(-18.5843617408396,-21.9792698628662,
10.4251105011625));
#214219=CARTESIAN_POINT('Ctrl Pts',(-21.1984585272586,-20.7164258552413,
10.5522863078439));
#214220=CARTESIAN_POINT('Ctrl Pts',(-21.5515675764649,-17.8348306380519,
10.6794621145253));
#214221=CARTESIAN_POINT('Ctrl Pts',(-19.319733252231,-15.9781689710992,
10.8066379212068));
#214222=CARTESIAN_POINT('Ctrl Pts',(-16.5505250237807,-16.849812696393,
10.9338137278882));
#214223=CARTESIAN_POINT('Ctrl Pts',(-15.7845195642707,-19.6500827962871,
11.0609895345697));
#214224=CARTESIAN_POINT('Ctrl Pts',(-17.7244793391404,-21.8099052584926,
11.1881653412511));
#214225=CARTESIAN_POINT('Ctrl Pts',(-20.5906116624301,-21.3477770276364,
11.3153411479325));
#214226=CARTESIAN_POINT('Ctrl Pts',(-21.753418019756,-18.6876720726163,
11.442516954614));
#214227=CARTESIAN_POINT('Ctrl Pts',(-20.1460957501734,-16.2700715849292,
11.5696927612954));
#214228=CARTESIAN_POINT('Ctrl Pts',(-17.2432632743535,-16.3129739588191,
11.6968685679768));
#214229=CARTESIAN_POINT('Ctrl Pts',(-15.7080892187581,-18.7770189290635,
11.8240443746583));
#214230=CARTESIAN_POINT('Ctrl Pts',(-16.9490004957481,-21.4015981713421,
11.9512201813397));
#214231=CARTESIAN_POINT('Ctrl Pts',(-19.8275380283252,-21.7788231306235,
12.0783959880211));
#214232=CARTESIAN_POINT('Ctrl Pts',(-21.7028222925386,-19.5626133199888,
12.2055717947026));
#214233=CARTESIAN_POINT('Ctrl Pts',(-20.8543963692405,-16.7862036872011,
12.332747601384));
#214234=CARTESIAN_POINT('Ctrl Pts',(-18.0606383838055,-15.996777746927,
12.4599234080654));
#214235=CARTESIAN_POINT('Ctrl Pts',(-15.8846478876935,-17.9185848020682,
12.5870992147468));
#214236=CARTESIAN_POINT('Ctrl Pts',(-16.3227611038855,-20.7884861603309,
12.7142750214283));
#214237=CARTESIAN_POINT('Ctrl Pts',(-18.9730363488984,-21.9735254516762,
12.8414508281097));
#214238=CARTESIAN_POINT('Ctrl Pts',(-21.404010580066,-20.3865026781285,
12.9686266347912));
#214239=CARTESIAN_POINT('Ctrl Pts',(-21.3854158235693,-17.4834127326752,
13.0958024414726));
#214240=CARTESIAN_POINT('Ctrl Pts',(-18.9343116143732,-15.9276604541869,
13.222978248154));
#214241=CARTESIAN_POINT('Ctrl Pts',(-16.2994339317307,-17.1465519972999,
13.3501540548355));
#214242=CARTESIAN_POINT('Ctrl Pts',(-15.8981195105134,-20.0218300241493,
13.4773298615169));
#214243=CARTESIAN_POINT('Ctrl Pts',(-18.0985494238061,-21.9156054049817,
13.6045056681983));
#214244=CARTESIAN_POINT('Ctrl Pts',(-20.8819658002459,-21.0904567688396,
13.7316814748798));
#214245=CARTESIAN_POINT('Ctrl Pts',(-21.694756872753,-18.3034067748831,
13.8588572815612));
#214246=CARTESIAN_POINT('Ctrl Pts',(-19.7912372798057,-16.1114008087357,
13.9860330882426));
#214247=CARTESIAN_POINT('Ctrl Pts',(-16.9177681021827,-16.5254682931038,
14.1132088949241));
#214248=CARTESIAN_POINT('Ctrl Pts',(-15.7105789627421,-19.1657280110059,
14.2403847016055));
#214249=CARTESIAN_POINT('Ctrl Pts',(-17.2771909703125,-21.6099055442666,
14.367560508287));
#214250=CARTESIAN_POINT('Ctrl Pts',(-20.1803348428554,-21.6156197088857,
14.4947363149684));
#214251=CARTESIAN_POINT('Ctrl Pts',(-21.7565562667429,-19.1776281134862,
14.6219121216498));
#214252=CARTESIAN_POINT('Ctrl Pts',(-20.5597699168931,-16.5326367280233,
14.7490879283312));
#214253=CARTESIAN_POINT('Ctrl Pts',(-17.6879529883551,-16.107260981979,
14.8762637350127));
#214254=CARTESIAN_POINT('Ctrl Pts',(-15.7758192680016,-18.2917567205529,
15.0034395416941));
#214255=CARTESIAN_POINT('Ctrl Pts',(-16.5776327638535,-21.0819846886999,
15.1306153483755));
#214256=CARTESIAN_POINT('Ctrl Pts',(-19.3577793596249,-21.9180839067241,
15.257791155057));
#214257=CARTESIAN_POINT('Ctrl Pts',(-21.5656471090539,-20.0329852362584,
15.3849669617384));
#214258=CARTESIAN_POINT('Ctrl Pts',(-21.1756543877665,-17.1561497050361,
15.5121427684199));
#214259=CARTESIAN_POINT('Ctrl Pts',(-18.545595311866,-15.9268953564031,
15.6393185751013));
#214260=CARTESIAN_POINT('Ctrl Pts',(-16.0883858436145,-17.4729867591009,
15.7664943817827));
#214261=CARTESIAN_POINT('Ctrl Pts',(-16.0583631585132,-20.3759810124089,
15.8936701884641));
#214262=CARTESIAN_POINT('Ctrl Pts',(-18.4830712067246,-21.9725610690611,
16.0208459951456));
#214263=CARTESIAN_POINT('Ctrl Pts',(-21.1379908483687,-20.7979638220132,
16.148021801827));
#214264=CARTESIAN_POINT('Ctrl Pts',(-21.5873980951341,-17.9298093417044,
16.2751976085084));
#214265=CARTESIAN_POINT('Ctrl Pts',(-19.418989691473,-15.9994513460744,
16.4023734151899));
#214266=CARTESIAN_POINT('Ctrl Pts',(-16.6221457611405,-16.7778734845843,
16.5295492218713));
#214267=CARTESIAN_POINT('Ctrl Pts',(-15.7627970185048,-19.550921759478,
16.6567250285528));
#214268=CARTESIAN_POINT('Ctrl Pts',(-17.6293425977359,-21.7744964933273,
16.7839008352342));
#214269=CARTESIAN_POINT('Ctrl Pts',(-20.5093427807734,-21.4086058784384,
16.9110766419156));
#214270=CARTESIAN_POINT('Ctrl Pts',(-21.7605761526514,-18.7889318442388,
17.0382524485971));
#214271=CARTESIAN_POINT('Ctrl Pts',(-20.2351137549734,-16.3188627217991,
17.1654282552785));
#214272=CARTESIAN_POINT('Ctrl Pts',(-17.3324726567343,-16.2645336211774,
17.2926040619599));
#214273=CARTESIAN_POINT('Ctrl Pts',(-15.7156459073444,-18.6757881201507,
17.4197798686414));
#214274=CARTESIAN_POINT('Ctrl Pts',(-16.8679716977821,-21.3404498752418,
17.5469556753228));
#214275=CARTESIAN_POINT('Ctrl Pts',(-19.7322626367279,-21.813857113719,
17.6741314820042));
#214276=CARTESIAN_POINT('Ctrl Pts',(-21.6807095656397,-19.6616880772395,
17.8013072886857));
#214277=CARTESIAN_POINT('Ctrl Pts',(-20.925733361505,-16.8584242781114,
17.9284830953671));
#214278=CARTESIAN_POINT('Ctrl Pts',(-18.1599778324925,-15.9758862618349,
18.0556589020486));
#214279=CARTESIAN_POINT('Ctrl Pts',(-15.9208520143557,-17.8237478819072,
18.18283470873));
#214280=CARTESIAN_POINT('Ctrl Pts',(-16.2626148693509,-20.7067107930414,
18.3100105154114));
#214281=CARTESIAN_POINT('Ctrl Pts',(-18.871720190335,-21.9798354613185,
18.4371863220928));
#214282=CARTESIAN_POINT('Ctrl Pts',(-21.3544757844137,-20.4751090222602,
18.5643621287743));
#214283=CARTESIAN_POINT('Ctrl Pts',(-21.4331074916559,-17.573024590546,
18.6915379354557));
#214284=CARTESIAN_POINT('Ctrl Pts',(-19.0354756002437,-15.9360645072522,
18.8187137421372));
#214285=CARTESIAN_POINT('Ctrl Pts',(-16.3612585583812,-17.0660380501958,
18.9458895488186));
#214286=CARTESIAN_POINT('Ctrl Pts',(-15.8638845181663,-19.926264622792,
19.0730653555));
#214287=CARTESIAN_POINT('Ctrl Pts',(-17.9996632971129,-21.8926638800028,
19.2002411621814));
#214288=CARTESIAN_POINT('Ctrl Pts',(-20.8091504151054,-21.1611865332722,
19.3274169688629));
#214289=CARTESIAN_POINT('Ctrl Pts',(-21.7148158405835,-18.4029176833963,
19.4545927755443));
#214290=CARTESIAN_POINT('Ctrl Pts',(-19.8857677137514,-16.1483977337339,
19.5817685822257));
#214291=CARTESIAN_POINT('Ctrl Pts',(-17.0000442519466,-16.4660089396223,
19.7089443889072));
#214292=CARTESIAN_POINT('Ctrl Pts',(-15.7051174603682,-19.0643624769379,
19.8361201955886));
#214293=CARTESIAN_POINT('Ctrl Pts',(-17.1890026117629,-21.5596307402518,
19.9632960022701));
#214294=CARTESIAN_POINT('Ctrl Pts',(-20.0903265756109,-21.6625590217998,
20.0904718089515));
#214295=CARTESIAN_POINT('Ctrl Pts',(-21.7473058561185,-19.2787188421125,
20.2176476156329));
#214296=CARTESIAN_POINT('Ctrl Pts',(-20.6397625633182,-16.5951320814986,
20.3448234223144));
#214297=CARTESIAN_POINT('Ctrl Pts',(-17.7838032497984,-16.0738298258407,
20.4719992289958));
#214298=CARTESIAN_POINT('Ctrl Pts',(-15.7995849948555,-18.1930614463123,
20.5991750356772));
#214299=CARTESIAN_POINT('Ctrl Pts',(-16.5075209429087,-21.0085886920376,
20.7263508423587));
#214300=CARTESIAN_POINT('Ctrl Pts',(-19.2580928765906,-21.9372914608301,
20.8535266490401));
#214301=CARTESIAN_POINT('Ctrl Pts',(-21.5278813506218,-20.1272362554868,
20.9807024557215));
#214302=CARTESIAN_POINT('Ctrl Pts',(-21.2343815144973,-17.2388559379038,
21.107878262403));
#214303=CARTESIAN_POINT('Ctrl Pts',(-18.647082453596,-15.9224078539418,
21.2350540690844));
#214304=CARTESIAN_POINT('Ctrl Pts',(-16.1392442526231,-17.3849814787741,
21.3622298757658));
#214305=CARTESIAN_POINT('Ctrl Pts',(-16.0124741552623,-20.2860474906393,
21.4894056824473));
#214306=CARTESIAN_POINT('Ctrl Pts',(-18.3814921015747,-21.9615662752975,
21.6165814891287));
#214307=CARTESIAN_POINT('Ctrl Pts',(-21.0759341658266,-20.8791897513666,
21.7437572958101));
#214308=CARTESIAN_POINT('Ctrl Pts',(-21.6178065999207,-18.0222756693125,
21.8709331024916));
#214309=CARTESIAN_POINT('Ctrl Pts',(-20.2210099178527,-16.6964452859245,
21.9557169736125));
#214310=CARTESIAN_POINT('Ctrl Pts',(-19.3965839472885,-16.475840953354,
21.998108909173));
#214311=CARTESIAN_POINT('Ctrl Pts',(-17.1140743056112,-17.5890877707427,
1.73472347597681E-18));
#214312=CARTESIAN_POINT('Ctrl Pts',(-17.0606037558837,-17.6406831599911,
2.50957526619234E-15));
#214313=CARTESIAN_POINT('Ctrl Pts',(-17.0102648206888,-17.6951284552545,
2.0073975135774E-14));
#214314=CARTESIAN_POINT('Ctrl Pts',(-16.9630512610728,-17.7520566525928,
1.3759826611448E-14));
#214315=CARTESIAN_POINT('Ctrl Pts',(-16.9139640310005,-17.811244045856,
7.39579948662126E-15));
#214316=CARTESIAN_POINT('Ctrl Pts',(-16.8682546395764,-17.873115719352,
-2.41757959083345E-14));
#214317=CARTESIAN_POINT('Ctrl Pts',(-16.8259443403958,-17.937308752054,
-1.47035161823794E-14));
#214318=CARTESIAN_POINT('Ctrl Pts',(-16.7856210013394,-17.9984871760508,
-5.6760700422245E-15));
#214319=CARTESIAN_POINT('Ctrl Pts',(-16.7483849217229,-18.061774974692,
4.48760828751193E-15));
#214320=CARTESIAN_POINT('Ctrl Pts',(-16.7142833600929,-18.1268912399334,
-5.97438765126412E-15));
#214321=CARTESIAN_POINT('Ctrl Pts',(-16.6917479443229,-18.1699221757752,
-1.29058387990152E-14));
#214322=CARTESIAN_POINT('Ctrl Pts',(-16.670581955631,-18.2137522504246,
-3.54114788609107E-14));
#214323=CARTESIAN_POINT('Ctrl Pts',(-16.6508067523184,-18.2583061596181,
-7.7715611723761E-15));
#214324=CARTESIAN_POINT('Ctrl Pts',(-16.6447946121616,-18.271851625744,
8.59586006653776E-16));
#214325=CARTESIAN_POINT('Ctrl Pts',(-16.6389106011744,-18.2854654139231,
1.30990802670221E-14));
#214326=CARTESIAN_POINT('Ctrl Pts',(-16.6331633226596,-18.2991259028343,
9.76302372279747E-15));
#214327=CARTESIAN_POINT('Ctrl Pts',(-16.6020274374077,-18.3731316107767,
-9.37108370488806E-15));
#214328=CARTESIAN_POINT('Ctrl Pts',(-16.5748437493431,-18.4486320984917,
-9.72962485609361E-16));
#214329=CARTESIAN_POINT('Ctrl Pts',(-16.5516340690814,-18.5252437971799,
1.88737914186277E-15));
#214330=CARTESIAN_POINT('Ctrl Pts',(-16.5281113691115,-18.602888727317,
4.78629705696217E-15));
#214331=CARTESIAN_POINT('Ctrl Pts',(-16.5086701130808,-18.6816758757728,
8.82622860769151E-15));
#214332=CARTESIAN_POINT('Ctrl Pts',(-16.4933735667248,-18.7612412026621,
7.36910532594948E-15));
#214333=CARTESIAN_POINT('Ctrl Pts',(-16.4780905784557,-18.8407360068606,
5.91327356475586E-15));
#214334=CARTESIAN_POINT('Ctrl Pts',(-16.4669445521086,-18.9210085588168,
-3.76344494961826E-15));
#214335=CARTESIAN_POINT('Ctrl Pts',(-16.4600452985084,-19.001717210151,
-8.72912853111529E-15));
#214336=CARTESIAN_POINT('Ctrl Pts',(-16.458249908906,-19.0227199854994,
-1.00213460937811E-14));
#214337=CARTESIAN_POINT('Ctrl Pts',(-16.4567423723362,-19.0437523637043,
-5.36502461302182E-15));
#214338=CARTESIAN_POINT('Ctrl Pts',(-16.4555251966164,-19.0648084381479,
2.56739074444567E-15));
#214339=CARTESIAN_POINT('Ctrl Pts',(-16.4546316923203,-19.0802652803004,
8.42156714837826E-15));
#214340=CARTESIAN_POINT('Ctrl Pts',(-16.4538946607534,-19.0957348924738,
2.92099871876547E-16));
#214341=CARTESIAN_POINT('Ctrl Pts',(-16.4533151797917,-19.1112149436894,
8.85402862138562E-15));
#214342=CARTESIAN_POINT('Ctrl Pts',(-16.4528674697077,-19.1231749138822,
1.55531854101286E-14));
#214343=CARTESIAN_POINT('Ctrl Pts',(-16.4525139746189,-19.1351378160613,
2.00079667589343E-14));
#214344=CARTESIAN_POINT('Ctrl Pts',(-16.4522551154433,-19.1470940326229,
1.58345558887163E-14));
#214345=CARTESIAN_POINT('Ctrl Pts',(-16.450448336251,-19.23054575209,-1.44011488464872E-14));
#214346=CARTESIAN_POINT('Ctrl Pts',(-16.4532433905666,-19.3137912323742,
-1.21694340773906E-14));
#214347=CARTESIAN_POINT('Ctrl Pts',(-16.4606965224471,-19.3964498394684,
-8.71525074330748E-15));
#214348=CARTESIAN_POINT('Ctrl Pts',(-16.4681353636814,-19.4789499568243,
-5.18520424887126E-15));
#214349=CARTESIAN_POINT('Ctrl Pts',(-16.4802140623254,-19.560866453353,
-1.0737231714089E-14));
#214350=CARTESIAN_POINT('Ctrl Pts',(-16.4970379007565,-19.6418365052423,
5.52335954751015E-15));
#214351=CARTESIAN_POINT('Ctrl Pts',(-16.5134756240274,-19.7209482556099,
2.1146494257637E-14));
#214352=CARTESIAN_POINT('Ctrl Pts',(-16.5344429618587,-19.7991574576156,
2.06622882565801E-14));
#214353=CARTESIAN_POINT('Ctrl Pts',(-16.5596742522225,-19.8762376297952,
9.2148511043888E-15));
#214354=CARTESIAN_POINT('Ctrl Pts',(-16.5700716763688,-19.9080011754509,
4.59487668223206E-15));
#214355=CARTESIAN_POINT('Ctrl Pts',(-16.5811937949009,-19.9395729260017,
-5.73054096894381E-15));
#214356=CARTESIAN_POINT('Ctrl Pts',(-16.593024502045,-19.9709365575929,
9.24260668000443E-15));
#214357=CARTESIAN_POINT('Ctrl Pts',(-16.599575769931,-19.9883042051838,
1.75753077980789E-14));
#214358=CARTESIAN_POINT('Ctrl Pts',(-16.6063465654584,-20.005613174688,
7.16385352924337E-15));
#214359=CARTESIAN_POINT('Ctrl Pts',(-16.6133217610784,-20.0228306160632,
1.08524300657109E-14));
#214360=CARTESIAN_POINT('Ctrl Pts',(-16.6442809363235,-20.0992496606094,
2.7032515933421E-14));
#214361=CARTESIAN_POINT('Ctrl Pts',(-16.6792960167752,-20.1739619594251,
1.93406742481452E-14));
#214362=CARTESIAN_POINT('Ctrl Pts',(-16.7180389842821,-20.246743899253,
5.35682609381638E-15));
#214363=CARTESIAN_POINT('Ctrl Pts',(-16.7588459173261,-20.3234031728317,
-9.3719877284186E-15));
#214364=CARTESIAN_POINT('Ctrl Pts',(-16.803788552284,-20.3979217843379,
-7.52420306717188E-15));
#214365=CARTESIAN_POINT('Ctrl Pts',(-16.8525440995263,-20.4700328123178,
7.57727214306669E-15));
#214366=CARTESIAN_POINT('Ctrl Pts',(-16.9012996467686,-20.5421438402977,
2.26787473533053E-14));
#214367=CARTESIAN_POINT('Ctrl Pts',(-16.9538687049381,-20.6118481705157,
1.06480511332545E-14));
#214368=CARTESIAN_POINT('Ctrl Pts',(-17.009981736112,-20.6788601850433,
-4.9960036108132E-15));
#214369=CARTESIAN_POINT('Ctrl Pts',(-17.0318954596463,-20.7050302694089,
-1.09832900983411E-14));
#214370=CARTESIAN_POINT('Ctrl Pts',(-17.0543502078806,-20.7307894693846,
3.40249426276482E-15));
#214371=CARTESIAN_POINT('Ctrl Pts',(-17.0773318266369,-20.7561195433156,
1.83186799063151E-14));
#214372=CARTESIAN_POINT('Ctrl Pts',(-17.0864635878594,-20.7661844647356,
2.42676587261844E-14));
#214373=CARTESIAN_POINT('Ctrl Pts',(-17.0956793012105,-20.776182428681,
2.64107502889692E-15));
#214374=CARTESIAN_POINT('Ctrl Pts',(-17.1049757714685,-20.7861097474567,
2.08166817117217E-15));
#214375=CARTESIAN_POINT('Ctrl Pts',(-17.1654853800672,-20.8507254733048,
-1.15724079903374E-15));
#214376=CARTESIAN_POINT('Ctrl Pts',(-17.2292147782235,-20.9121401114294,
1.62919071033182E-14));
#214377=CARTESIAN_POINT('Ctrl Pts',(-17.2958558788046,-20.9700792980957,
1.88737914186277E-15));
#214378=CARTESIAN_POINT('Ctrl Pts',(-17.3510487696017,-21.0180651682969,
-1.00426089860209E-14));
#214379=CARTESIAN_POINT('Ctrl Pts',(-17.4082400170084,-21.063667078019,
2.71337193772128E-14));
#214380=CARTESIAN_POINT('Ctrl Pts',(-17.4672777570143,-21.1067151950334,
5.63438184997267E-15));
#214381=CARTESIAN_POINT('Ctrl Pts',(-17.4867746670186,-21.1209316142798,
-1.5378003559757E-15));
#214382=CARTESIAN_POINT('Ctrl Pts',(-17.5064731111025,-21.1348693857667,
3.24666800846887E-14));
#214383=CARTESIAN_POINT('Ctrl Pts',(-17.5263680478785,-21.1485219846966,
2.39808173319034E-14));
#214384=CARTESIAN_POINT('Ctrl Pts',(-17.5422931318004,-21.1594503322534,
1.70518113475176E-14));
#214385=CARTESIAN_POINT('Ctrl Pts',(-17.5583454808324,-21.1701967133747,
2.25387075678082E-14));
#214386=CARTESIAN_POINT('Ctrl Pts',(-17.574506564613,-21.1807476004758,
2.41195952099815E-14));
#214387=CARTESIAN_POINT('Ctrl Pts',(-17.6490343637846,-21.2294036439462,
3.11874514914716E-14));
#214388=CARTESIAN_POINT('Ctrl Pts',(-17.7259442979181,-21.2739559986071,
3.27197442341185E-14));
#214389=CARTESIAN_POINT('Ctrl Pts',(-17.804955500985,-21.3141140597646,
1.57929225252929E-14));
#214390=CARTESIAN_POINT('Ctrl Pts',(-17.8827967354047,-21.3536774752179,
-1.3531531152433E-15));
#214391=CARTESIAN_POINT('Ctrl Pts',(-17.9626781499771,-21.3889764950412,
4.75096733707754E-15));
#214392=CARTESIAN_POINT('Ctrl Pts',(-18.0443636118602,-21.4196958725292,
-4.38538094726937E-15));
#214393=CARTESIAN_POINT('Ctrl Pts',(-18.0530583776972,-21.4229657052236,
-5.14211066895245E-15));
#214394=CARTESIAN_POINT('Ctrl Pts',(-18.0617736083461,-21.4261836096314,
-1.19767995287112E-14));
#214395=CARTESIAN_POINT('Ctrl Pts',(-18.0705088883292,-21.4293497159892,
1.11022302462516E-16));
#214396=CARTESIAN_POINT('Ctrl Pts',(-19.3965839546295,-21.4281590740807,
0.00189110722368242));
#214397=CARTESIAN_POINT('Ctrl Pts',(-20.2210099343281,-21.207554739066,
0.0442830427841606));
#214398=CARTESIAN_POINT('Ctrl Pts',(-21.6178066866466,-19.8817246731204,
0.129066913905116));
#214399=CARTESIAN_POINT('Ctrl Pts',(-21.0759341432978,-17.0248100445211,
0.256242720586551));
#214400=CARTESIAN_POINT('Ctrl Pts',(-18.381492106794,-15.9424338299618,
0.383418527267985));
#214401=CARTESIAN_POINT('Ctrl Pts',(-16.0124741472572,-17.6179524340247,
0.51059433394942));
#214402=CARTESIAN_POINT('Ctrl Pts',(-16.1392442377966,-20.5190185688902,
0.637770140630853));
#214403=CARTESIAN_POINT('Ctrl Pts',(-18.6470824574045,-21.9815921336574,
0.764945947312289));
#214404=CARTESIAN_POINT('Ctrl Pts',(-21.2343815212355,-20.6651440828081,
0.892121753993721));
#214405=CARTESIAN_POINT('Ctrl Pts',(-21.5278813636115,-17.7767637319101,
1.01929756067515));
#214406=CARTESIAN_POINT('Ctrl Pts',(-19.2580928773362,-15.966708532015,
1.14647336735659));
#214407=CARTESIAN_POINT('Ctrl Pts',(-16.5075209349949,-16.8954112973593,
1.27364917403802));
#214408=CARTESIAN_POINT('Ctrl Pts',(-15.7995849828837,-19.7109385580857,
1.40082498071946));
#214409=CARTESIAN_POINT('Ctrl Pts',(-17.7838032463622,-21.8301701846349,
1.52800078740089));
#214410=CARTESIAN_POINT('Ctrl Pts',(-20.6397625706149,-21.308867928169,
1.65517659408233));
#214411=CARTESIAN_POINT('Ctrl Pts',(-21.7473058680116,-18.6252811563658,
1.78235240076376));
#214412=CARTESIAN_POINT('Ctrl Pts',(-20.0903265808676,-16.2414409677205,
1.9095282074452));
#214413=CARTESIAN_POINT('Ctrl Pts',(-17.1890026057441,-16.3443692494651,
2.03670401412663));
#214414=CARTESIAN_POINT('Ctrl Pts',(-15.7051174484919,-18.839637522662,
2.16387982080806));
#214415=CARTESIAN_POINT('Ctrl Pts',(-17.000044245167,-21.4379910700896,
2.2910556274895));
#214416=CARTESIAN_POINT('Ctrl Pts',(-19.8857677182557,-21.7556022772552,
2.41823143417093));
#214417=CARTESIAN_POINT('Ctrl Pts',(-21.7148158522574,-19.5010823187472,
2.54540724085237));
#214418=CARTESIAN_POINT('Ctrl Pts',(-20.8091504232289,-16.7428134580815,
2.6725830475338));
#214419=CARTESIAN_POINT('Ctrl Pts',(-17.9996632942386,-16.0113361084815,
2.79975885421524));
#214420=CARTESIAN_POINT('Ctrl Pts',(-15.8638845069282,-17.9777353733943,
2.92693466089667));
#214421=CARTESIAN_POINT('Ctrl Pts',(-16.3612585490912,-20.837961957188,
3.0541104675781));
#214422=CARTESIAN_POINT('Ctrl Pts',(-19.035475601424,-21.9679355045566,
3.18128627425954));
#214423=CARTESIAN_POINT('Ctrl Pts',(-21.433107502224,-20.3309754148531,
3.30846208094097));
#214424=CARTESIAN_POINT('Ctrl Pts',(-21.354475794674,-17.4288909717763,
3.43563788762241));
#214425=CARTESIAN_POINT('Ctrl Pts',(-18.8717201908742,-15.9241645268262,
3.56281369430384));
#214426=CARTESIAN_POINT('Ctrl Pts',(-16.2626148596744,-17.1972892000883,
3.68998950098528));
#214427=CARTESIAN_POINT('Ctrl Pts',(-15.920852003341,-20.0802521225103,
3.8171653076667));
#214428=CARTESIAN_POINT('Ctrl Pts',(-18.1599778302449,-21.9281137498178,
3.94434111434815));
#214429=CARTESIAN_POINT('Ctrl Pts',(-20.9257333700864,-21.0455757300857,
4.07151692102957));
#214430=CARTESIAN_POINT('Ctrl Pts',(-21.6807095771773,-18.2423119199819,
4.19869272771102));
#214431=CARTESIAN_POINT('Ctrl Pts',(-19.7322626406367,-16.0901428750757,
4.32586853439245));
#214432=CARTESIAN_POINT('Ctrl Pts',(-16.867971690476,-16.5635501154064,
4.45304434107388));
#214433=CARTESIAN_POINT('Ctrl Pts',(-15.7156458955263,-19.2282118809307,
4.58022014775532));
#214434=CARTESIAN_POINT('Ctrl Pts',(-17.3324726512467,-21.639466389345,
4.70739595443675));
#214435=CARTESIAN_POINT('Ctrl Pts',(-20.2351137608509,-21.5851372885107,
4.83457176111819));
#214436=CARTESIAN_POINT('Ctrl Pts',(-21.7605761645016,-19.1150681563998,
4.96174756779962));
#214437=CARTESIAN_POINT('Ctrl Pts',(-20.5093427877246,-16.4953941119431,
5.08892337448106));
#214438=CARTESIAN_POINT('Ctrl Pts',(-17.6293425934107,-16.1295034956214,
5.21609918116249));
#214439=CARTESIAN_POINT('Ctrl Pts',(-15.7627970068714,-18.353078238177,
5.34327498784392));
#214440=CARTESIAN_POINT('Ctrl Pts',(-16.6221457528718,-21.1261265239282,
5.47045079452535));
#214441=CARTESIAN_POINT('Ctrl Pts',(-19.418989694155,-21.904548665486,5.5976266012068));
#214442=CARTESIAN_POINT('Ctrl Pts',(-21.5873981063063,-19.974190662298,
5.72480240788822));
#214443=CARTESIAN_POINT('Ctrl Pts',(-21.1379908577814,-17.1060361707592,
5.85197821456966));
#214444=CARTESIAN_POINT('Ctrl Pts',(-18.4830712057421,-15.9314389191122,
5.97915402125109));
#214445=CARTESIAN_POINT('Ctrl Pts',(-16.0583631480371,-17.5280189820156,
6.10632982793253));
#214446=CARTESIAN_POINT('Ctrl Pts',(-16.0883858332559,-20.43101324669,6.23350563461397));
#214447=CARTESIAN_POINT('Ctrl Pts',(-18.5455953111282,-21.9771046554414,
6.3606814412954));
#214448=CARTESIAN_POINT('Ctrl Pts',(-21.1756543973266,-20.7478503019954,
6.48785724797683));
#214449=CARTESIAN_POINT('Ctrl Pts',(-21.5656471201409,-17.8710147595092,
6.61503305465826));
#214450=CARTESIAN_POINT('Ctrl Pts',(-19.3577793620672,-15.9859160816625,
6.74220886133971));
#214451=CARTESIAN_POINT('Ctrl Pts',(-16.5776327554104,-16.8220153029603,
6.86938466802113));
#214452=CARTESIAN_POINT('Ctrl Pts',(-15.7758192564191,-19.6122432820323,
6.99656047470258));
#214453=CARTESIAN_POINT('Ctrl Pts',(-17.6879529842593,-21.7967390291592,
7.123736281384));
#214454=CARTESIAN_POINT('Ctrl Pts',(-20.5597699240417,-21.3713632814495,
7.25091208806544));
#214455=CARTESIAN_POINT('Ctrl Pts',(-21.7565562785773,-18.7263718856303,
7.37808789474687));
#214456=CARTESIAN_POINT('Ctrl Pts',(-20.1803348485183,-16.2883802806852,
7.50526370142831));
#214457=CARTESIAN_POINT('Ctrl Pts',(-17.2771909646086,-16.2940944453266,
7.63243950810973));
#214458=CARTESIAN_POINT('Ctrl Pts',(-15.7105789509042,-18.7382719881573,
7.75961531479118));
#214459=CARTESIAN_POINT('Ctrl Pts',(-16.9177680950714,-21.3785317163971,
7.8867911214726));
#214460=CARTESIAN_POINT('Ctrl Pts',(-19.7912372839452,-21.7925992023863,
8.01396692815404));
#214461=CARTESIAN_POINT('Ctrl Pts',(-21.6947568843456,-19.6005932276563,
8.14114273483548));
#214462=CARTESIAN_POINT('Ctrl Pts',(-20.8819658086561,-16.8135432227874,
8.26831854151691));
#214463=CARTESIAN_POINT('Ctrl Pts',(-18.098549421318,-15.9883945834145,
8.39549434819835));
#214464=CARTESIAN_POINT('Ctrl Pts',(-15.8981194994098,-17.8821699716618,
8.52267015487978));
#214465=CARTESIAN_POINT('Ctrl Pts',(-16.2994339221984,-20.7574480097692,
8.64984596156122));
#214466=CARTESIAN_POINT('Ctrl Pts',(-18.9343116151575,-21.9763395576547,
8.77702176824265));
#214467=CARTESIAN_POINT('Ctrl Pts',(-21.3854158339506,-20.4205872730748,
8.90419757492408));
#214468=CARTESIAN_POINT('Ctrl Pts',(-21.4040105905201,-17.5174973162549,
9.03137338160553));
#214469=CARTESIAN_POINT('Ctrl Pts',(-18.9730363498343,-15.9304745364933,
9.15854918828694));
#214470=CARTESIAN_POINT('Ctrl Pts',(-16.3227610944446,-17.1155138324785,
9.28572499496839));
#214471=CARTESIAN_POINT('Ctrl Pts',(-15.884647876537,-19.985415201978,9.41290080164982));
#214472=CARTESIAN_POINT('Ctrl Pts',(-18.060638381169,-21.9072222646439,
9.54007660833126));
#214473=CARTESIAN_POINT('Ctrl Pts',(-20.8543963775427,-21.1177963212788,
9.66725241501268));
#214474=CARTESIAN_POINT('Ctrl Pts',(-21.7028223041627,-18.3413866776205,
9.79442822169412));
#214475=CARTESIAN_POINT('Ctrl Pts',(-19.8275380326068,-16.1251768583083,
9.92160402837557));
#214476=CARTESIAN_POINT('Ctrl Pts',(-16.949000488759,-16.5024018190668,
10.048779835057));
#214477=CARTESIAN_POINT('Ctrl Pts',(-15.7080892069104,-19.1269810716216,
10.1759556417385));
#214478=CARTESIAN_POINT('Ctrl Pts',(-17.2432632685167,-21.5910260515137,
10.3031314484199));
#214479=CARTESIAN_POINT('Ctrl Pts',(-20.1460957557023,-21.6339284255716,
10.4303072551013));
#214480=CARTESIAN_POINT('Ctrl Pts',(-21.7534180315782,-19.2163279284187,
10.5574830617828));
#214481=CARTESIAN_POINT('Ctrl Pts',(-20.5906116696995,-16.5562229629832,
10.6846588684642));
#214482=CARTESIAN_POINT('Ctrl Pts',(-17.7244793351877,-16.0940947303175,
10.8118346751456));
#214483=CARTESIAN_POINT('Ctrl Pts',(-15.7845195527222,-18.2539172009796,
10.9390104818271));
#214484=CARTESIAN_POINT('Ctrl Pts',(-16.5505250152316,-21.0541873118379,
11.0661862885085));
#214485=CARTESIAN_POINT('Ctrl Pts',(-19.3197332545243,-21.9258310405445,
11.1933620951899));
#214486=CARTESIAN_POINT('Ctrl Pts',(-21.5515675874969,-20.0691693663223,
11.3205379018714));
#214487=CARTESIAN_POINT('Ctrl Pts',(-21.1984585369079,-17.1875741378502,
11.4477137085528));
#214488=CARTESIAN_POINT('Ctrl Pts',(-18.5843617402537,-15.9247301252809,
11.5748895152342));
#214489=CARTESIAN_POINT('Ctrl Pts',(-16.1075487593188,-17.4392183292074,
11.7020653219157));
#214490=CARTESIAN_POINT('Ctrl Pts',(-16.04034177576,-20.3415898222665,11.8292411285971));
#214491=CARTESIAN_POINT('Ctrl Pts',(-18.4443990256569,-21.9690989010672,
11.9564169352785));
#214492=CARTESIAN_POINT('Ctrl Pts',(-21.1141471948498,-20.828607000416,
12.08359274196));
#214493=CARTESIAN_POINT('Ctrl Pts',(-21.6002580413636,-17.9664446522494,
12.2107685486414));
#214494=CARTESIAN_POINT('Ctrl Pts',(-19.4567550349637,-16.0084681651805,
12.3379443553228));
#214495=CARTESIAN_POINT('Ctrl Pts',(-16.6501691432213,-16.7509994403685,
12.4651201620043));
#214496=CARTESIAN_POINT('Ctrl Pts',(-15.7553687254437,-19.512812119517,
12.5922959686857));
#214497=CARTESIAN_POINT('Ctrl Pts',(-17.5932776273647,-21.7601144869345,
12.7194717753671));
#214498=CARTESIAN_POINT('Ctrl Pts',(-20.4777285049632,-21.431146103831,
12.8466475820486));
#214499=CARTESIAN_POINT('Ctrl Pts',(-21.7624167072548,-18.8277150436234,
12.97382338873));
#214500=CARTESIAN_POINT('Ctrl Pts',(-20.2687205453794,-16.3383077168971,
13.1009991954114));
#214501=CARTESIAN_POINT('Ctrl Pts',(-17.3670135386182,-16.2468008358791,
13.2281750020929));
#214502=CARTESIAN_POINT('Ctrl Pts',(-15.7194317654263,-18.6371462843459,
13.3553508087743));
#214503=CARTESIAN_POINT('Ctrl Pts',(-16.8375292422496,-21.3163504748999,
13.4825266154557));
#214504=CARTESIAN_POINT('Ctrl Pts',(-19.6955209310585,-21.8264098528738,
13.6097024221372));
#214505=CARTESIAN_POINT('Ctrl Pts',(-21.6713768443407,-19.699376596832,
13.7368782288186));
#214506=CARTESIAN_POINT('Ctrl Pts',(-20.9523718171085,-16.8866717006199,
13.8640540355001));
#214507=CARTESIAN_POINT('Ctrl Pts',(-18.1981483353624,-15.9687773303578,
13.9912298421815));
#214508=CARTESIAN_POINT('Ctrl Pts',(-15.9355354972161,-17.7878045998115,
14.1184056488629));
#214509=CARTESIAN_POINT('Ctrl Pts',(-16.240340148078,-20.6749088908223,
14.2455814555443));
#214510=CARTESIAN_POINT('Ctrl Pts',(-18.8329229390928,-21.9813512102896,
14.3727572622258));
#214511=CARTESIAN_POINT('Ctrl Pts',(-21.3347500733399,-20.5085518170573,
14.4999330689072));
#214512=CARTESIAN_POINT('Ctrl Pts',(-21.450550436052,-17.6077127421763,
14.6271088755887));
#214513=CARTESIAN_POINT('Ctrl Pts',(-19.0740843818219,-15.9401737904716,
14.7542846822701));
#214514=CARTESIAN_POINT('Ctrl Pts',(-16.3856120152874,-17.0357984509923,
14.8814604889515));
#214515=CARTESIAN_POINT('Ctrl Pts',(-15.85163986733,-19.8894190998463,15.008636295633));
#214516=CARTESIAN_POINT('Ctrl Pts',(-17.9620542416513,-21.8830159073825,
15.1358121023144));
#214517=CARTESIAN_POINT('Ctrl Pts',(-20.7806809369003,-21.1875875392591,
15.2629879089958));
#214518=CARTESIAN_POINT('Ctrl Pts',(-21.7216049038886,-18.441146360077,
15.3901637156773));
#214519=CARTESIAN_POINT('Ctrl Pts',(-19.9215868032322,-16.1633816883713,
15.5173395223587));
#214520=CARTESIAN_POINT('Ctrl Pts',(-17.0320315205603,-16.4440012364127,
15.6445153290401));
#214521=CARTESIAN_POINT('Ctrl Pts',(-15.7039266816969,-19.0255539860864,
15.7716911357216));
#214522=CARTESIAN_POINT('Ctrl Pts',(-17.1557260448163,-21.5396255188012,
15.898866942403));
#214523=CARTESIAN_POINT('Ctrl Pts',(-20.0554938030875,-21.6797112441684,
16.0260427490844));
#214524=CARTESIAN_POINT('Ctrl Pts',(-21.7428730181815,-19.3172912038646,
16.1532185557659));
#214525=CARTESIAN_POINT('Ctrl Pts',(-20.6697979908152,-16.6197391565441,
16.2803943624473));
#214526=CARTESIAN_POINT('Ctrl Pts',(-17.8207484560495,-16.0618916766609,
16.4075701691287));
#214527=CARTESIAN_POINT('Ctrl Pts',(-15.8095505300749,-18.1555392030885,
16.5347459758102));
#214528=CARTESIAN_POINT('Ctrl Pts',(-16.4813534809519,-20.9798900767501,
16.6619217824916));
#214529=CARTESIAN_POINT('Ctrl Pts',(-19.2198197980441,-21.9437776700467,
16.789097589173));
#214530=CARTESIAN_POINT('Ctrl Pts',(-21.5125766038083,-20.1628949417396,
16.9162733958545));
#214531=CARTESIAN_POINT('Ctrl Pts',(-21.2561618334919,-17.2710912610025,
17.0434492025359));
#214532=CARTESIAN_POINT('Ctrl Pts',(-18.6858201239648,-15.9214170193332,
17.1706250092173));
#214533=CARTESIAN_POINT('Ctrl Pts',(-16.1596804603196,-17.3521145632324,
17.2978008158988));
#214534=CARTESIAN_POINT('Ctrl Pts',(-15.9953191940406,-20.2506076952764,
17.4249766225802));
#214535=CARTESIAN_POINT('Ctrl Pts',(-18.3435275855282,-21.9577088675884,
17.5521524292616));
#214536=CARTESIAN_POINT('Ctrl Pts',(-21.0499701818423,-20.9072587092191,
17.6793282359431));
#214537=CARTESIAN_POINT('Ctrl Pts',(-21.631653881637,-18.0629800421848,
17.8065040426245));
#214538=CARTESIAN_POINT('Ctrl Pts',(-19.5549199937129,-16.0343220076414,
17.933679849306));
#214539=CARTESIAN_POINT('Ctrl Pts',(-16.725042963598,-16.6824524395731,
18.0608556559873));
#214540=CARTESIAN_POINT('Ctrl Pts',(-15.7382593244464,-19.4127518941776,
18.1880314626688));
#214541=CARTESIAN_POINT('Ctrl Pts',(-17.4998818184781,-21.7203400833824,
18.3152072693502));
#214542=CARTESIAN_POINT('Ctrl Pts',(-20.3937311460449,-21.4881480686078,
18.4423830760317));
#214543=CARTESIAN_POINT('Ctrl Pts',(-21.7648801616449,-18.9291976120636,
18.5695588827131));
#214544=CARTESIAN_POINT('Ctrl Pts',(-20.3553847465806,-16.3911669310282,
18.6967346893946));
#214545=CARTESIAN_POINT('Ctrl Pts',(-17.4583694610031,-16.2025416478318,
18.823910496076));
#214546=CARTESIAN_POINT('Ctrl Pts',(-15.7316660204183,-18.5363737515732,
18.9510863027574));
#214547=CARTESIAN_POINT('Ctrl Pts',(-16.7594176601915,-21.2515171426226,
19.0782621094388));
#214548=CARTESIAN_POINT('Ctrl Pts',(-19.5987260404249,-21.8569962774213,
19.2054379161203));
#214549=CARTESIAN_POINT('Ctrl Pts',(-21.6447019493503,-19.7973216359904,
19.3326137228017));
#214550=CARTESIAN_POINT('Ctrl Pts',(-21.0202894786101,-16.9621168526002,
19.4597895294832));
#214551=CARTESIAN_POINT('Ctrl Pts',(-18.2983483137461,-15.9525063653534,
19.5869653361646));
#214552=CARTESIAN_POINT('Ctrl Pts',(-15.9760905326363,-17.6947450904228,
19.714141142846));
#214553=CARTESIAN_POINT('Ctrl Pts',(-16.184043510336,-20.5904372147467,
19.8413169495275));
#214554=CARTESIAN_POINT('Ctrl Pts',(-18.7314233036429,-21.9829647838468,
19.9684927562089));
#214555=CARTESIAN_POINT('Ctrl Pts',(-21.2811670472796,-20.5947704862204,
20.0956685628903));
#214556=CARTESIAN_POINT('Ctrl Pts',(-21.49404313672,-17.6994358448221,20.2228443695718));
#214557=CARTESIAN_POINT('Ctrl Pts',(-19.1747509237061,-15.9532518137242,
20.3500201762532));
#214558=CARTESIAN_POINT('Ctrl Pts',(-16.4510971561478,-16.9582316928714,
20.4771959829346));
#214559=CARTESIAN_POINT('Ctrl Pts',(-15.8218649356901,-19.7923729967134,
20.6043717896161));
#214560=CARTESIAN_POINT('Ctrl Pts',(-17.8643361189216,-21.8555189367891,
20.7315475962975));
#214561=CARTESIAN_POINT('Ctrl Pts',(-20.704669493102,-21.2548766742021,
20.8587234029789));
#214562=CARTESIAN_POINT('Ctrl Pts',(-21.7370367735022,-18.5414683255483,
20.9858992096604));
#214563=CARTESIAN_POINT('Ctrl Pts',(-20.0143025609789,-16.2047352065647,
21.1130750163418));
#214564=CARTESIAN_POINT('Ctrl Pts',(-17.1169733783673,-16.3883740006192,
21.2402508230232));
#214565=CARTESIAN_POINT('Ctrl Pts',(-15.7031596587772,-18.9241212228848,
21.3674266297047));
#214566=CARTESIAN_POINT('Ctrl Pts',(-17.0699655881192,-21.4851744179203,
21.4946024363861));
#214567=CARTESIAN_POINT('Ctrl Pts',(-19.963397156019,-21.7227196345909,
21.6217782430676));
#214568=CARTESIAN_POINT('Ctrl Pts',(-21.7289768951727,-19.4172948235399,
21.748954049749));
#214569=CARTESIAN_POINT('Ctrl Pts',(-20.7467658607354,-16.6869340105708,
21.8761298564304));
#214570=CARTESIAN_POINT('Ctrl Pts',(-17.9181415113151,-16.0308544058051,
22.0033056631118));
#214571=CARTESIAN_POINT('Ctrl Pts',(-15.8372814923396,-18.0626244799711,
22.1305001261329));
#214572=CARTESIAN_POINT('Ctrl Pts',(-16.2233207480177,-19.9500078885456,
22.2153026535935));
#214573=CARTESIAN_POINT('Ctrl Pts',(-16.7733104792501,-20.6030838137515,
22.2577132454937));
#214574=CARTESIAN_POINT('Ctrl Pts',(-19.3578031896578,-21.2832305070458,
-0.084727284346428));
#214575=CARTESIAN_POINT('Ctrl Pts',(-20.1339758575579,-21.0755380525683,
-0.0423353487859499));
#214576=CARTESIAN_POINT('Ctrl Pts',(-21.4490186733577,-19.8273082723234,
0.0424485223350063));
#214577=CARTESIAN_POINT('Ctrl Pts',(-20.9388617059771,-17.1376076759719,
0.169624329016441));
#214578=CARTESIAN_POINT('Ctrl Pts',(-18.4021242480669,-16.1185824938283,
0.296800135697875));
#214579=CARTESIAN_POINT('Ctrl Pts',(-16.1717639304198,-17.6960336866052,
0.42397594237931));
#214580=CARTESIAN_POINT('Ctrl Pts',(-16.2911142199628,-20.4273016198123,
0.551151749060743));
#214581=CARTESIAN_POINT('Ctrl Pts',(-18.6521697052435,-21.8042713584183,
0.678327555742179));
#214582=CARTESIAN_POINT('Ctrl Pts',(-21.0880352243816,-20.5648744678046,
0.805503362423611));
#214583=CARTESIAN_POINT('Ctrl Pts',(-21.3643566423075,-17.8455498248734,
0.932679169105048));
#214584=CARTESIAN_POINT('Ctrl Pts',(-19.2274179378702,-16.1414364076047,
1.05985497578648));
#214585=CARTESIAN_POINT('Ctrl Pts',(-16.6378358343089,-17.0157825839918,
1.18703078246792));
#214586=CARTESIAN_POINT('Ctrl Pts',(-15.9713350808349,-19.6665181980038,
1.31420658914935));
#214587=CARTESIAN_POINT('Ctrl Pts',(-17.8394178695693,-21.6617120734788,
1.44138239583079));
#214588=CARTESIAN_POINT('Ctrl Pts',(-20.5282190751429,-21.1709214225929,
1.56855820251222));
#214589=CARTESIAN_POINT('Ctrl Pts',(-21.5709383211686,-18.6444038752278,
1.69573400919365));
#214590=CARTESIAN_POINT('Ctrl Pts',(-20.0109413467548,-16.4000888674147,
1.82290981587509));
#214591=CARTESIAN_POINT('Ctrl Pts',(-17.2794306645736,-16.4969927993764,
1.95008562255652));
#214592=CARTESIAN_POINT('Ctrl Pts',(-15.882396692181,-18.8462140520133,
2.07726142923796));
#214593=CARTESIAN_POINT('Ctrl Pts',(-17.1015319587312,-21.2924870403926,
2.20443723591939));
#214594=CARTESIAN_POINT('Ctrl Pts',(-19.8183552298129,-21.5915085948938,
2.33161304260083));
#214595=CARTESIAN_POINT('Ctrl Pts',(-21.5403499326061,-19.4689447576054,
2.45878884928226));
#214596=CARTESIAN_POINT('Ctrl Pts',(-20.6876927267632,-16.8721162331674,
2.5859646559637));
#214597=CARTESIAN_POINT('Ctrl Pts',(-18.0426437180737,-16.1834519504684,
2.71314046264513));
#214598=CARTESIAN_POINT('Ctrl Pts',(-16.0318711803166,-18.0347586792573,
2.84031626932657));
#214599=CARTESIAN_POINT('Ctrl Pts',(-16.5001341253916,-20.7275773834348,
2.967492076008));
#214600=CARTESIAN_POINT('Ctrl Pts',(-19.0178303590937,-21.7914140461736,
3.09466788268943));
#214601=CARTESIAN_POINT('Ctrl Pts',(-21.2751298558503,-20.2502645538495,
3.22184368937087));
#214602=CARTESIAN_POINT('Ctrl Pts',(-21.201100429639,-17.5180379135899,
3.3490194960523));
#214603=CARTESIAN_POINT('Ctrl Pts',(-18.8636594850319,-16.1013824854533,
3.47619530273374));
#214604=CARTESIAN_POINT('Ctrl Pts',(-16.40726401034,-17.2999916978614,3.60337110941517));
#214605=CARTESIAN_POINT('Ctrl Pts',(-16.0855043927131,-20.0142159921659,
3.73054691609661));
#214606=CARTESIAN_POINT('Ctrl Pts',(-18.1935751105569,-21.7539230422786,
3.85772272277804));
#214607=CARTESIAN_POINT('Ctrl Pts',(-20.7974521219332,-20.9230396080263,
3.98489852945948));
#214608=CARTESIAN_POINT('Ctrl Pts',(-21.5082398837079,-18.2838496699412,
4.11207433614091));
#214609=CARTESIAN_POINT('Ctrl Pts',(-19.6738347409324,-16.2576461895902,
4.23925014282234));
#214610=CARTESIAN_POINT('Ctrl Pts',(-16.9771895560713,-16.703345099837,
4.36642594950377));
#214611=CARTESIAN_POINT('Ctrl Pts',(-15.8923089135627,-19.2120453137177,
4.49360175618521));
#214612=CARTESIAN_POINT('Ctrl Pts',(-17.4145034676192,-21.482170092496,
4.62077756286664));
#214613=CARTESIAN_POINT('Ctrl Pts',(-20.1472541929444,-21.4310208514753,
4.74795336954808));
#214614=CARTESIAN_POINT('Ctrl Pts',(-21.5834319126906,-19.1055238446132,
4.87512917622951));
#214615=CARTESIAN_POINT('Ctrl Pts',(-20.4054327082334,-16.6391782390827,
5.00230498291095));
#214616=CARTESIAN_POINT('Ctrl Pts',(-17.6939977347856,-16.2947030492859,
5.12948078959238));
#214617=CARTESIAN_POINT('Ctrl Pts',(-15.9367002898516,-18.3881328813199,
5.25665659627382));
#214618=CARTESIAN_POINT('Ctrl Pts',(-16.7457517089779,-20.9988757972025,
5.38383240295525));
#214619=CARTESIAN_POINT('Ctrl Pts',(-19.3788975305108,-21.7317372125915,
5.51100820963669));
#214620=CARTESIAN_POINT('Ctrl Pts',(-21.4203898946547,-19.914362265377,
5.63818401631812));
#214621=CARTESIAN_POINT('Ctrl Pts',(-20.9972862666143,-17.2140796706178,
5.76535982299955));
#214622=CARTESIAN_POINT('Ctrl Pts',(-18.4977579643435,-16.1082311105657,
5.89253562968099));
#214623=CARTESIAN_POINT('Ctrl Pts',(-16.2149670669532,-17.6113640023665,
6.01971143636243));
#214624=CARTESIAN_POINT('Ctrl Pts',(-16.2432325368166,-20.3444472127417,
6.14688724304385));
#214625=CARTESIAN_POINT('Ctrl Pts',(-18.5566225596869,-21.8000465304473,
6.2740630497253));
#214626=CARTESIAN_POINT('Ctrl Pts',(-21.0327453747589,-20.6427399261711,
6.40123885640672));
#214627=CARTESIAN_POINT('Ctrl Pts',(-21.3999119847184,-17.9342843787876,
6.52841466308816));
#214628=CARTESIAN_POINT('Ctrl Pts',(-19.3212698138575,-16.1595197473112,
6.6555904697696));
#214629=CARTESIAN_POINT('Ctrl Pts',(-16.7038440388577,-16.9466824268052,
6.78276627645102));
#214630=CARTESIAN_POINT('Ctrl Pts',(-15.9489603525162,-19.57359951566,6.90994208313247));
#214631=CARTESIAN_POINT('Ctrl Pts',(-17.7491776836857,-21.6302376297137,
7.03711788981389));
#214632=CARTESIAN_POINT('Ctrl Pts',(-20.452908365107,-21.2297589486797,
7.16429369649533));
#214633=CARTESIAN_POINT('Ctrl Pts',(-21.5796473090278,-18.7395778058964,
7.29146950317678));
#214634=CARTESIAN_POINT('Ctrl Pts',(-20.0956814677067,-16.4442808417949,
7.41864530985819));
#214635=CARTESIAN_POINT('Ctrl Pts',(-17.3624573952481,-16.4496605587419,
7.54582111653964));
#214636=CARTESIAN_POINT('Ctrl Pts',(-15.8875385351148,-18.7507814003416,
7.67299692322106));
#214637=CARTESIAN_POINT('Ctrl Pts',(-17.0240713976901,-21.236507818093,
7.80017272990251));
#214638=CARTESIAN_POINT('Ctrl Pts',(-19.7293576227465,-21.6263401052905,
7.92734853658393));
#214639=CARTESIAN_POINT('Ctrl Pts',(-21.5214650077943,-19.5626313341509,
8.05452434326538));
#214640=CARTESIAN_POINT('Ctrl Pts',(-20.756246257781,-16.9387062139828,
8.1817001499468));
#214641=CARTESIAN_POINT('Ctrl Pts',(-18.1357420810118,-16.1618531833802,
8.30887595662825));
#214642=CARTESIAN_POINT('Ctrl Pts',(-16.06410241284,-17.9447866809843,8.43605176330966));
#214643=CARTESIAN_POINT('Ctrl Pts',(-16.4419280683544,-20.6517758840763,
8.56322756999113));
#214644=CARTESIAN_POINT('Ctrl Pts',(-18.9225874591253,-21.7993262135178,
8.69040337667253));
#214645=CARTESIAN_POINT('Ctrl Pts',(-21.2302295612066,-20.3346314670524,
8.81757918335399));
#214646=CARTESIAN_POINT('Ctrl Pts',(-21.2477359743606,-17.6014581653534,
8.94475499003541));
#214647=CARTESIAN_POINT('Ctrl Pts',(-18.9590456510891,-16.1073231728629,
9.07193079671685));
#214648=CARTESIAN_POINT('Ctrl Pts',(-16.4638899108517,-17.2230026087143,
9.19910660339829));
#214649=CARTESIAN_POINT('Ctrl Pts',(-16.0514192784853,-19.9249298373897,
9.32628241007971));
#214650=CARTESIAN_POINT('Ctrl Pts',(-18.1000499583713,-21.7342543270959,
9.45345821676116));
#214651=CARTESIAN_POINT('Ctrl Pts',(-20.7302904540745,-20.9910331578707,
9.58063402344258));
#214652=CARTESIAN_POINT('Ctrl Pts',(-21.5290583619236,-18.3771256229697,
9.70780983012403));
#214653=CARTESIAN_POINT('Ctrl Pts',(-19.7635337035947,-16.2906296482662,
9.83498563680544));
#214654=CARTESIAN_POINT('Ctrl Pts',(-17.0534757722859,-16.6457757880052,
9.9621614434869));
#214655=CARTESIAN_POINT('Ctrl Pts',(-15.8851945148077,-19.1167395018316,
10.0893372501683));
#214656=CARTESIAN_POINT('Ctrl Pts',(-17.3305154731838,-21.4365649476141,
10.2165130568498));
#214657=CARTESIAN_POINT('Ctrl Pts',(-20.0634463748397,-21.4769562634529,
10.3436888635312));
#214658=CARTESIAN_POINT('Ctrl Pts',(-21.5766927423282,-19.2008569240337,
10.4708646702126));
#214659=CARTESIAN_POINT('Ctrl Pts',(-20.4819449561405,-16.6964468026162,
10.598040476894));
#214660=CARTESIAN_POINT('Ctrl Pts',(-17.7835661623932,-16.2613667443784,
10.7252162835755));
#214661=CARTESIAN_POINT('Ctrl Pts',(-15.9571514240733,-18.2947756986395,
10.8523920902569));
#214662=CARTESIAN_POINT('Ctrl Pts',(-16.678322903506,-20.9311471574582,
10.9795678969384));
#214663=CARTESIAN_POINT('Ctrl Pts',(-19.2854505292619,-21.7517739390354,
11.1067437036198));
#214664=CARTESIAN_POINT('Ctrl Pts',(-21.3866565212999,-20.0037819051163,
11.2339195103012));
#214665=CARTESIAN_POINT('Ctrl Pts',(-21.0542147974772,-17.2908452542003,
11.3610953169827));
#214666=CARTESIAN_POINT('Ctrl Pts',(-18.5931200057406,-16.1019149796642,
11.4882711236641));
#214667=CARTESIAN_POINT('Ctrl Pts',(-16.2612738647384,-17.5277608150597,
11.6154469303455));
#214668=CARTESIAN_POINT('Ctrl Pts',(-16.198000478146,-20.2602577043845,
11.742622737027));
#214669=CARTESIAN_POINT('Ctrl Pts',(-18.4613492509727,-21.7925093495675,
11.8697985437084));
#214670=CARTESIAN_POINT('Ctrl Pts',(-20.9748381634178,-20.7187699684155,
11.9969743503898));
#214671=CARTESIAN_POINT('Ctrl Pts',(-21.4324971430291,-18.0241287993538,
12.1241501570713));
#214672=CARTESIAN_POINT('Ctrl Pts',(-19.4144524815328,-16.1807518667032,
12.2513259637527));
#214673=CARTESIAN_POINT('Ctrl Pts',(-16.7721349018743,-16.879823093295,
12.3785017704341));
#214674=CARTESIAN_POINT('Ctrl Pts',(-15.9297067826652,-19.4799880179848,
12.5056775771156));
#214675=CARTESIAN_POINT('Ctrl Pts',(-17.6600436362941,-21.5957567068059,
12.632853383797));
#214676=CARTESIAN_POINT('Ctrl Pts',(-20.3756687963737,-21.2860427071796,
12.7600291904784));
#214677=CARTESIAN_POINT('Ctrl Pts',(-21.5851647292373,-18.8349893907445,
12.8872049971599));
#214678=CARTESIAN_POINT('Ctrl Pts',(-20.1788939862666,-16.4912860458039,
13.0143808038413));
#214679=CARTESIAN_POINT('Ctrl Pts',(-17.4470226911311,-16.4051350247055,
13.1415566105228));
#214680=CARTESIAN_POINT('Ctrl Pts',(-15.8958731980624,-18.6555745421719,
13.2687324172041));
#214681=CARTESIAN_POINT('Ctrl Pts',(-16.9485288917557,-21.1779660189567,
13.3959082238856));
#214682=CARTESIAN_POINT('Ctrl Pts',(-19.6392435084281,-21.6581718323812,
13.523084030567));
#214683=CARTESIAN_POINT('Ctrl Pts',(-21.4994533918664,-19.6556329535628,
13.6502598372485));
#214684=CARTESIAN_POINT('Ctrl Pts',(-20.8225314316626,-17.0075545122368,
13.7774356439299));
#214685=CARTESIAN_POINT('Ctrl Pts',(-18.2295115117883,-16.1433841200358,
13.9046114506113));
#214686=CARTESIAN_POINT('Ctrl Pts',(-16.0993284677614,-17.8559444753405,
14.0317872572928));
#214687=CARTESIAN_POINT('Ctrl Pts',(-16.3862930284057,-20.5740677456421,
14.1589630639742));
#214688=CARTESIAN_POINT('Ctrl Pts',(-18.8271330203595,-21.8040445361958,
14.2861388706557));
#214689=CARTESIAN_POINT('Ctrl Pts',(-21.1825292466206,-20.4174474826375,
14.4133146773371));
#214690=CARTESIAN_POINT('Ctrl Pts',(-21.2915518619716,-17.686393319688,
14.5404904840185));
#214691=CARTESIAN_POINT('Ctrl Pts',(-19.0541793835346,-16.1164547335152,
14.6676662907));
#214692=CARTESIAN_POINT('Ctrl Pts',(-16.5230621932784,-17.1479529355545,
14.7948420973814));
#214693=CARTESIAN_POINT('Ctrl Pts',(-16.0203432144126,-19.8345523474337,
14.9220179040628));
#214694=CARTESIAN_POINT('Ctrl Pts',(-18.0072359077879,-21.7114647579188,
15.0491937107442));
#214695=CARTESIAN_POINT('Ctrl Pts',(-20.6608895477009,-21.0567395247122,
15.1763695174257));
#214696=CARTESIAN_POINT('Ctrl Pts',(-21.5467416238517,-18.4710464124499,
15.3035453241071));
#214697=CARTESIAN_POINT('Ctrl Pts',(-19.8520778385523,-16.3265983654185,
15.4307211307886));
#214698=CARTESIAN_POINT('Ctrl Pts',(-17.1316470321183,-16.5907933673128,
15.55789693747));
#214699=CARTESIAN_POINT('Ctrl Pts',(-15.8812756204742,-19.0212489016859,
15.6850727441514));
#214700=CARTESIAN_POINT('Ctrl Pts',(-17.2481017670014,-21.3881728668337,
15.8122485508329));
#214701=CARTESIAN_POINT('Ctrl Pts',(-19.9781473170593,-21.5200594326025,
15.9394243575143));
#214702=CARTESIAN_POINT('Ctrl Pts',(-21.5667649242067,-19.295910860703,
16.0666001641957));
#214703=CARTESIAN_POINT('Ctrl Pts',(-20.5564965346144,-16.7562454196237,
16.1937759708772));
#214704=CARTESIAN_POINT('Ctrl Pts',(-17.8742006914056,-16.2310485221405,
16.3209517775586));
#214705=CARTESIAN_POINT('Ctrl Pts',(-15.9807173486685,-18.2021557242983,
16.44812758424));
#214706=CARTESIAN_POINT('Ctrl Pts',(-16.6131999505341,-20.8611985088279,
16.5753033909215));
#214707=CARTESIAN_POINT('Ctrl Pts',(-19.1913849660881,-21.7686701597314,
16.7024791976029));
#214708=CARTESIAN_POINT('Ctrl Pts',(-21.349947663769,-20.0920217613478,
16.8296550042843));
#214709=CARTESIAN_POINT('Ctrl Pts',(-21.1085407439649,-17.369474154658,
16.9568308109658));
#214710=CARTESIAN_POINT('Ctrl Pts',(-18.688640072193,-16.0987957884381,
17.0840066176472));
#214711=CARTESIAN_POINT('Ctrl Pts',(-16.3103543188293,-17.4457551965009,
17.2111824243287));
#214712=CARTESIAN_POINT('Ctrl Pts',(-16.1556130495236,-20.174600723678,
17.3383582310101));
#214713=CARTESIAN_POINT('Ctrl Pts',(-18.3663817745373,-21.7817859700398,
17.4655340376915));
#214714=CARTESIAN_POINT('Ctrl Pts',(-20.9144174044528,-20.7928182252147,
17.5927098443729));
#214715=CARTESIAN_POINT('Ctrl Pts',(-21.4620553977494,-18.1150140128212,
17.7198856510544));
#214716=CARTESIAN_POINT('Ctrl Pts',(-19.506871885825,-16.2050924944522,
17.8470614577358));
#214717=CARTESIAN_POINT('Ctrl Pts',(-16.8426263884951,-16.8152881201209,
17.9742372644172));
#214718=CARTESIAN_POINT('Ctrl Pts',(-15.9135987878357,-19.3857842762726,
18.1014130710987));
#214719=CARTESIAN_POINT('Ctrl Pts',(-17.5721142454945,-21.5583102826521,
18.2285888777801));
#214720=CARTESIAN_POINT('Ctrl Pts',(-20.2965877681507,-21.339708370521,
18.3557646844615));
#214721=CARTESIAN_POINT('Ctrl Pts',(-21.5874839986603,-18.9305322264037,
18.482940491143));
#214722=CARTESIAN_POINT('Ctrl Pts',(-20.2604857675958,-16.5410514319824,
18.6101162978244));
#214723=CARTESIAN_POINT('Ctrl Pts',(-17.5330315891426,-16.3634663086393,
18.7372921045058));
#214724=CARTESIAN_POINT('Ctrl Pts',(-15.907391387167,-18.560700184086,18.8644679111873));
#214725=CARTESIAN_POINT('Ctrl Pts',(-16.8749891483064,-21.1169273548174,
18.9916437178687));
#214726=CARTESIAN_POINT('Ctrl Pts',(-19.5481139827311,-21.6869680461436,
19.1188195245502));
#214727=CARTESIAN_POINT('Ctrl Pts',(-21.4743397674531,-19.7478453100669,
19.2459953312316));
#214728=CARTESIAN_POINT('Ctrl Pts',(-20.8864739005117,-17.0785838906586,
19.373171137913));
#214729=CARTESIAN_POINT('Ctrl Pts',(-18.323846826857,-16.1280654878871,
19.5003469445945));
#214730=CARTESIAN_POINT('Ctrl Pts',(-16.1375098337227,-17.7683317005682,
19.6275227512759));
#214731=CARTESIAN_POINT('Ctrl Pts',(-16.3332914095993,-20.4945401618491,
19.7546985579573));
#214732=CARTESIAN_POINT('Ctrl Pts',(-18.7315741166155,-21.8055636679596,
19.8818743646388));
#214733=CARTESIAN_POINT('Ctrl Pts',(-21.1320824129259,-20.4986198087347,
20.0090501713202));
#214734=CARTESIAN_POINT('Ctrl Pts',(-21.3324989528482,-17.7727479070516,
20.1362259780016));
#214735=CARTESIAN_POINT('Ctrl Pts',(-19.1489539543349,-16.1287673054729,
20.2634017846831));
#214736=CARTESIAN_POINT('Ctrl Pts',(-16.5847145159137,-17.0749261277227,
20.3905775913645));
#214737=CARTESIAN_POINT('Ctrl Pts',(-15.9923109972134,-19.7431863126012,
20.5177533980459));
#214738=CARTESIAN_POINT('Ctrl Pts',(-17.9152371863878,-21.6855771736479,
20.6449292047274));
#214739=CARTESIAN_POINT('Ctrl Pts',(-20.5893270222873,-21.1200902544022,
20.7721050114088));
#214740=CARTESIAN_POINT('Ctrl Pts',(-21.5612702725159,-18.5654965747524,
20.8992808180902));
#214741=CARTESIAN_POINT('Ctrl Pts',(-19.9393669813241,-16.3655314792863,
21.0264566247717));
#214742=CARTESIAN_POINT('Ctrl Pts',(-17.2116172781004,-16.5384219706357,
21.1536324314531));
#214743=CARTESIAN_POINT('Ctrl Pts',(-15.8805534910891,-18.9257529561851,
21.2808082381345));
#214744=CARTESIAN_POINT('Ctrl Pts',(-17.1673608343839,-21.3369087663789,
21.407984044816));
#214745=CARTESIAN_POINT('Ctrl Pts',(-19.8914410486737,-21.560550559712,
21.5351598514974));
#214746=CARTESIAN_POINT('Ctrl Pts',(-21.5536821355334,-19.3900613098573,
21.6623356581788));
#214747=CARTESIAN_POINT('Ctrl Pts',(-20.6289595069245,-16.8195073866206,
21.7895114648603));
#214748=CARTESIAN_POINT('Ctrl Pts',(-17.965893371406,-16.2018278499181,
21.9166872715417));
#214749=CARTESIAN_POINT('Ctrl Pts',(-16.006825229175,-18.1146792615168,
22.0438817345628));
#214750=CARTESIAN_POINT('Ctrl Pts',(-16.3702697667955,-19.8915948993761,
22.1286842620234));
#214751=CARTESIAN_POINT('Ctrl Pts',(-16.8880688264084,-20.506446560642,
22.1710948539236));
#214752=CARTESIAN_POINT('Ctrl Pts',(-19.3190224246859,-21.138301940011,
-0.171345675916538));
#214753=CARTESIAN_POINT('Ctrl Pts',(-20.0469417807877,-20.9435213660705,
-0.12895374035606));
#214754=CARTESIAN_POINT('Ctrl Pts',(-21.2802306600689,-19.7728918715264,
-0.0441698692351041));
#214755=CARTESIAN_POINT('Ctrl Pts',(-20.8017892686562,-17.2504053074226,
0.0830059374463301));
#214756=CARTESIAN_POINT('Ctrl Pts',(-18.42275638934,-16.2947311576948,0.210181744127764));
#214757=CARTESIAN_POINT('Ctrl Pts',(-16.3310537135823,-17.7741149391859,
0.337357550809199));
#214758=CARTESIAN_POINT('Ctrl Pts',(-16.4429842021291,-20.3355846707344,
0.464533357490633));
#214759=CARTESIAN_POINT('Ctrl Pts',(-18.6572569530825,-21.6269505831793,
0.591709164172068));
#214760=CARTESIAN_POINT('Ctrl Pts',(-20.9416889275276,-20.4646048528009,
0.718884970853502));
#214761=CARTESIAN_POINT('Ctrl Pts',(-21.2008319210033,-17.9143359178367,
0.846060777534936));
#214762=CARTESIAN_POINT('Ctrl Pts',(-19.1967429984043,-16.3161642831945,
0.973236584216371));
#214763=CARTESIAN_POINT('Ctrl Pts',(-16.7681507336229,-17.1361538706243,
1.1004123908978));
#214764=CARTESIAN_POINT('Ctrl Pts',(-16.1430851787862,-19.6220978379218,
1.22758819757924));
#214765=CARTESIAN_POINT('Ctrl Pts',(-17.8950324927765,-21.4932539623228,
1.35476400426067));
#214766=CARTESIAN_POINT('Ctrl Pts',(-20.4166755796707,-21.0329749170169,
1.48193981094211));
#214767=CARTESIAN_POINT('Ctrl Pts',(-21.3945707743255,-18.6635265940897,
1.60911561762354));
#214768=CARTESIAN_POINT('Ctrl Pts',(-19.9315561126419,-16.558736767109,
1.73629142430498));
#214769=CARTESIAN_POINT('Ctrl Pts',(-17.369858723403,-16.6496163492876,
1.86346723098641));
#214770=CARTESIAN_POINT('Ctrl Pts',(-16.0596759358701,-18.8527905813645,
1.99064303766784));
#214771=CARTESIAN_POINT('Ctrl Pts',(-17.2030196722955,-21.1469830106956,
2.11781884434928));
#214772=CARTESIAN_POINT('Ctrl Pts',(-19.7509427413702,-21.4274149125326,
2.24499465103071));
#214773=CARTESIAN_POINT('Ctrl Pts',(-21.3658840129548,-19.4368071964635,
2.37217045771215));
#214774=CARTESIAN_POINT('Ctrl Pts',(-20.5662350302976,-17.0014190082534,
2.49934626439358));
#214775=CARTESIAN_POINT('Ctrl Pts',(-18.0856241419088,-16.3555677924553,
2.62652207107501));
#214776=CARTESIAN_POINT('Ctrl Pts',(-16.1998578537051,-18.0917819851203,
2.75369787775646));
#214777=CARTESIAN_POINT('Ctrl Pts',(-16.639009701692,-20.6171928096815,
2.88087368443788));
#214778=CARTESIAN_POINT('Ctrl Pts',(-19.0001851167635,-21.6148925877907,
3.00804949111932));
#214779=CARTESIAN_POINT('Ctrl Pts',(-21.1171522094764,-20.169553692846,
3.13522529780075));
#214780=CARTESIAN_POINT('Ctrl Pts',(-21.0477250646041,-17.6071848554035,
3.26240110448218));
#214781=CARTESIAN_POINT('Ctrl Pts',(-18.8555987791894,-16.2786004440803,
3.38957691116362));
#214782=CARTESIAN_POINT('Ctrl Pts',(-16.5519131610055,-17.4026941956347,
3.51675271784505));
#214783=CARTESIAN_POINT('Ctrl Pts',(-16.2501567820852,-19.9481798618215,
3.64392852452649));
#214784=CARTESIAN_POINT('Ctrl Pts',(-18.2271723908689,-21.5797323347394,
3.77110433120793));
#214785=CARTESIAN_POINT('Ctrl Pts',(-20.6691708737799,-20.8005034859668,
3.89828013788936));
#214786=CARTESIAN_POINT('Ctrl Pts',(-21.3357701902385,-18.3253874199006,
4.02545594457079));
#214787=CARTESIAN_POINT('Ctrl Pts',(-19.6154068412282,-16.4251495041048,
4.15263175125223));
#214788=CARTESIAN_POINT('Ctrl Pts',(-17.0864074216668,-16.8431400842676,
4.27980755793366));
#214789=CARTESIAN_POINT('Ctrl Pts',(-16.068971931599,-19.1958787465047,
4.4069833646151));
#214790=CARTESIAN_POINT('Ctrl Pts',(-17.4965342839917,-21.3248737956469,
4.53415917129653));
#214791=CARTESIAN_POINT('Ctrl Pts',(-20.0593946250379,-21.2769044144401,
4.66133497797797));
#214792=CARTESIAN_POINT('Ctrl Pts',(-21.4062876608796,-19.0959795328267,
4.7885107846594));
#214793=CARTESIAN_POINT('Ctrl Pts',(-20.3015226287422,-16.7829623662223,
4.91568659134084));
#214794=CARTESIAN_POINT('Ctrl Pts',(-17.7586528761605,-16.4599026029505,
5.04286239802226));
#214795=CARTESIAN_POINT('Ctrl Pts',(-16.1106035728318,-18.4231875244628,
5.17003820470371));
#214796=CARTESIAN_POINT('Ctrl Pts',(-16.8693576650841,-20.8716250704767,
5.29721401138513));
#214797=CARTESIAN_POINT('Ctrl Pts',(-19.3388053668663,-21.5589257596971,
5.42438981806658));
#214798=CARTESIAN_POINT('Ctrl Pts',(-21.2533816830032,-19.8545338684562,
5.551565624748));
#214799=CARTESIAN_POINT('Ctrl Pts',(-20.8565816754472,-17.3221231704762,
5.67874143142944));
#214800=CARTESIAN_POINT('Ctrl Pts',(-18.5124447229449,-16.2850233020193,
5.80591723811088));
#214801=CARTESIAN_POINT('Ctrl Pts',(-16.3715709858693,-17.6947090227174,
5.93309304479231));
#214802=CARTESIAN_POINT('Ctrl Pts',(-16.3980792403773,-20.2578811787933,
6.06026885147374));
#214803=CARTESIAN_POINT('Ctrl Pts',(-18.5676498082457,-21.6229884054533,
6.18744465815518));
#214804=CARTESIAN_POINT('Ctrl Pts',(-20.8898363521913,-20.5376295503469,
6.31462046483661));
#214805=CARTESIAN_POINT('Ctrl Pts',(-21.234176849296,-17.9975539980662,
6.44179627151804));
#214806=CARTESIAN_POINT('Ctrl Pts',(-19.2847602656477,-16.33312341296,6.56897207819949));
#214807=CARTESIAN_POINT('Ctrl Pts',(-16.830055322305,-17.0713495506502,
6.6961478848809));
#214808=CARTESIAN_POINT('Ctrl Pts',(-16.1221014486134,-19.5349557492877,
6.82332369156236));
#214809=CARTESIAN_POINT('Ctrl Pts',(-17.810402383112,-21.4637362302682,
6.95049949824377));
#214810=CARTESIAN_POINT('Ctrl Pts',(-20.3460468061722,-21.0881546159098,
7.07767530492523));
#214811=CARTESIAN_POINT('Ctrl Pts',(-21.4027383394782,-18.7527837261624,
7.20485111160664));
#214812=CARTESIAN_POINT('Ctrl Pts',(-20.0110280868951,-16.6001814029045,
7.3320269182881));
#214813=CARTESIAN_POINT('Ctrl Pts',(-17.4477238258878,-16.6052266721572,
7.45920272496951));
#214814=CARTESIAN_POINT('Ctrl Pts',(-16.0644981193252,-18.7632908125259,
7.58637853165096));
#214815=CARTESIAN_POINT('Ctrl Pts',(-17.130374700309,-21.0944839197888,
7.71355433833239));
#214816=CARTESIAN_POINT('Ctrl Pts',(-19.6674779615479,-21.4600810081947,
7.84073014501382));
#214817=CARTESIAN_POINT('Ctrl Pts',(-21.3481731312431,-19.5246694406454,
7.96790595169526));
#214818=CARTESIAN_POINT('Ctrl Pts',(-20.630526706906,-17.0638692051782,
8.09508175837669));
#214819=CARTESIAN_POINT('Ctrl Pts',(-18.1729347407055,-16.3353117833461,
8.22225756505813));
#214820=CARTESIAN_POINT('Ctrl Pts',(-16.2300853262702,-18.0074033903068,
8.34943337173957));
#214821=CARTESIAN_POINT('Ctrl Pts',(-16.5844222145103,-20.5461037583834,
8.47660917842099));
#214822=CARTESIAN_POINT('Ctrl Pts',(-18.910863303093,-21.622312869381,8.60378498510243));
#214823=CARTESIAN_POINT('Ctrl Pts',(-21.0750432884624,-20.2486756610299,
8.73096079178387));
#214824=CARTESIAN_POINT('Ctrl Pts',(-21.091461358201,-17.685419014452,8.8581365984653));
#214825=CARTESIAN_POINT('Ctrl Pts',(-18.9450549523438,-16.2841718092325,
8.98531240514673));
#214826=CARTESIAN_POINT('Ctrl Pts',(-16.6050187272589,-17.3304913849503,
9.11248821182817));
#214827=CARTESIAN_POINT('Ctrl Pts',(-16.2181906804335,-19.8644444728012,
9.2396640185096));
#214828=CARTESIAN_POINT('Ctrl Pts',(-18.1394615355737,-21.561286389548,
9.36683982519104));
#214829=CARTESIAN_POINT('Ctrl Pts',(-20.6061845306062,-20.8642699944625,
9.49401563187247));
#214830=CARTESIAN_POINT('Ctrl Pts',(-21.3552944196844,-18.4128645683191,
9.62119143855391));
#214831=CARTESIAN_POINT('Ctrl Pts',(-19.6995293745825,-16.4560824382241,
9.74836724523534));
#214832=CARTESIAN_POINT('Ctrl Pts',(-17.1579510558127,-16.7891497569436,
9.87554305191677));
#214833=CARTESIAN_POINT('Ctrl Pts',(-16.062299822705,-19.1064979320416,
10.0027188585982));
#214834=CARTESIAN_POINT('Ctrl Pts',(-17.417767677851,-21.2821038437145,
10.1298946652796));
#214835=CARTESIAN_POINT('Ctrl Pts',(-19.9807969939772,-21.3199841013343,
10.257070471961));
#214836=CARTESIAN_POINT('Ctrl Pts',(-21.3999674530782,-19.1853859196488,
10.3842462786425));
#214837=CARTESIAN_POINT('Ctrl Pts',(-20.3732782425814,-16.8366706422493,
10.5114220853239));
#214838=CARTESIAN_POINT('Ctrl Pts',(-17.8426529895985,-16.4286387584391,
10.6385978920053));
#214839=CARTESIAN_POINT('Ctrl Pts',(-16.1297832954242,-18.3356341962992,
10.7657736986868));
#214840=CARTESIAN_POINT('Ctrl Pts',(-16.8061207917803,-20.8081070030786,
10.8929495053682));
#214841=CARTESIAN_POINT('Ctrl Pts',(-19.2511678039994,-21.5777168375263,
11.0201253120496));
#214842=CARTESIAN_POINT('Ctrl Pts',(-21.221745455103,-19.9383944439102,
11.1473011187311));
#214843=CARTESIAN_POINT('Ctrl Pts',(-20.9099710580464,-17.3941163705504,
11.2744769254125));
#214844=CARTESIAN_POINT('Ctrl Pts',(-18.6018782712276,-16.2790998340474,
11.401652732094));
#214845=CARTESIAN_POINT('Ctrl Pts',(-16.414998970158,-17.6163033009118,
11.5288285387754));
#214846=CARTESIAN_POINT('Ctrl Pts',(-16.3556591805319,-20.1789255865028,
11.6560043454568));
#214847=CARTESIAN_POINT('Ctrl Pts',(-18.4782994762885,-21.6159197980676,
11.7831801521383));
#214848=CARTESIAN_POINT('Ctrl Pts',(-20.8355291319859,-20.6089329364152,
11.9103559588197));
#214849=CARTESIAN_POINT('Ctrl Pts',(-21.2647362446946,-18.0818129464581,
12.0375317655011));
#214850=CARTESIAN_POINT('Ctrl Pts',(-19.372149928102,-16.3530355682261,
12.1647075721826));
#214851=CARTESIAN_POINT('Ctrl Pts',(-16.8941006605274,-17.0086467462216,
12.291883378864));
#214852=CARTESIAN_POINT('Ctrl Pts',(-16.1040448398867,-19.4471639164527,
12.4190591855454));
#214853=CARTESIAN_POINT('Ctrl Pts',(-17.7268096452235,-21.4313989266772,
12.5462349922269));
#214854=CARTESIAN_POINT('Ctrl Pts',(-20.2736090877839,-21.1409393105282,
12.6734107989083));
#214855=CARTESIAN_POINT('Ctrl Pts',(-21.4079127512197,-18.8422637378655,
12.8005866055897));
#214856=CARTESIAN_POINT('Ctrl Pts',(-20.0890674271536,-16.6442643747106,
12.9277624122712));
#214857=CARTESIAN_POINT('Ctrl Pts',(-17.5270318436439,-16.563469213532,
13.0549382189526));
#214858=CARTESIAN_POINT('Ctrl Pts',(-16.0723146306984,-18.6740027999979,
13.182114025634));
#214859=CARTESIAN_POINT('Ctrl Pts',(-17.0595285412618,-21.0395815630135,
13.3092898323155));
#214860=CARTESIAN_POINT('Ctrl Pts',(-19.5829660857976,-21.4899338118888,
13.4364656389969));
#214861=CARTESIAN_POINT('Ctrl Pts',(-21.3275299393921,-19.6118893102937,
13.5636414456783));
#214862=CARTESIAN_POINT('Ctrl Pts',(-20.6926910462166,-17.1284373238537,
13.6908172523598));
#214863=CARTESIAN_POINT('Ctrl Pts',(-18.2608746882143,-16.3179909097138,
13.8179930590412));
#214864=CARTESIAN_POINT('Ctrl Pts',(-16.2631214383067,-17.9240843508695,
13.9451688657226));
#214865=CARTESIAN_POINT('Ctrl Pts',(-16.5322459087333,-20.4732266004621,
14.0723446724041));
#214866=CARTESIAN_POINT('Ctrl Pts',(-18.8213431016262,-21.6267378621019,
14.1995204790855));
#214867=CARTESIAN_POINT('Ctrl Pts',(-21.0303084199013,-20.3263431482177,
14.326696285767));
#214868=CARTESIAN_POINT('Ctrl Pts',(-21.1325532878912,-17.7650738971998,
14.4538720924484));
#214869=CARTESIAN_POINT('Ctrl Pts',(-19.0342743852475,-16.2927356765588,
14.5810478991298));
#214870=CARTESIAN_POINT('Ctrl Pts',(-16.6605123712694,-17.2601074201168,
14.7082237058113));
#214871=CARTESIAN_POINT('Ctrl Pts',(-16.1890465614952,-19.779685595021,
14.8353995124927));
#214872=CARTESIAN_POINT('Ctrl Pts',(-18.0524175739244,-21.5399136084552,
14.9625753191741));
#214873=CARTESIAN_POINT('Ctrl Pts',(-20.5410981585017,-20.9258915101652,
15.0897511258555));
#214874=CARTESIAN_POINT('Ctrl Pts',(-21.3718783438148,-18.5009464648227,
15.216926932537));
#214875=CARTESIAN_POINT('Ctrl Pts',(-19.7825688738725,-16.4898150424656,
15.3441027392184));
#214876=CARTESIAN_POINT('Ctrl Pts',(-17.2312625436763,-16.7375854982129,
15.4712785458999));
#214877=CARTESIAN_POINT('Ctrl Pts',(-16.0586245592516,-19.0169438172852,
15.5984543525813));
#214878=CARTESIAN_POINT('Ctrl Pts',(-17.3404774891864,-21.2367202148663,
15.7256301592627));
#214879=CARTESIAN_POINT('Ctrl Pts',(-19.9008008310311,-21.3604076210367,
15.8528059659442));
#214880=CARTESIAN_POINT('Ctrl Pts',(-21.3906568302317,-19.2745305175414,
15.9799817726256));
#214881=CARTESIAN_POINT('Ctrl Pts',(-20.4431950784138,-16.8927516827034,
16.107157579307));
#214882=CARTESIAN_POINT('Ctrl Pts',(-17.9276529267619,-16.40020536762,16.2343333859885));
#214883=CARTESIAN_POINT('Ctrl Pts',(-16.1518841672621,-18.2487722455082,
16.3615091926699));
#214884=CARTESIAN_POINT('Ctrl Pts',(-16.7450464201164,-20.7425069409056,
16.4886849993513));
#214885=CARTESIAN_POINT('Ctrl Pts',(-19.1629501341323,-21.5935626494162,
16.6158608060327));
#214886=CARTESIAN_POINT('Ctrl Pts',(-21.1873187237296,-20.0211485809561,
16.7430366127142));
#214887=CARTESIAN_POINT('Ctrl Pts',(-20.9609196544379,-17.4678570483134,
16.8702124193956));
#214888=CARTESIAN_POINT('Ctrl Pts',(-18.6914600204213,-16.276174557543,
16.9973882260771));
#214889=CARTESIAN_POINT('Ctrl Pts',(-16.4610281773391,-17.5393958297695,
17.1245640327585));
#214890=CARTESIAN_POINT('Ctrl Pts',(-16.3159069050066,-20.0985937520796,
17.2517398394399));
#214891=CARTESIAN_POINT('Ctrl Pts',(-18.3892359635466,-21.6058630724912,
17.3789156461214));
#214892=CARTESIAN_POINT('Ctrl Pts',(-20.7788646270633,-20.6783777412105,
17.5060914528028));
#214893=CARTESIAN_POINT('Ctrl Pts',(-21.2924569138618,-18.1670479834574,
17.6332672594842));
#214894=CARTESIAN_POINT('Ctrl Pts',(-19.458823777937,-16.375862981263,17.7604430661657));
#214895=CARTESIAN_POINT('Ctrl Pts',(-16.9602098133921,-16.9481238006687,
17.8876188728471));
#214896=CARTESIAN_POINT('Ctrl Pts',(-16.0889382512251,-19.3588166583677,
18.0147946795285));
#214897=CARTESIAN_POINT('Ctrl Pts',(-17.6443466725109,-21.3962804819219,
18.14197048621));
#214898=CARTESIAN_POINT('Ctrl Pts',(-20.1994443902567,-21.1912686724342,
18.2691462928914));
#214899=CARTESIAN_POINT('Ctrl Pts',(-21.4100878356756,-18.9318668407438,
18.3963220995729));
#214900=CARTESIAN_POINT('Ctrl Pts',(-20.1655867886111,-16.6909359329365,
18.5234979062543));
#214901=CARTESIAN_POINT('Ctrl Pts',(-17.607693717282,-16.5243909694468,
18.6506737129357));
#214902=CARTESIAN_POINT('Ctrl Pts',(-16.0831167539157,-18.5850266165988,
18.7778495196171));
#214903=CARTESIAN_POINT('Ctrl Pts',(-16.9905606364213,-20.9823375670122,
18.9050253262986));
#214904=CARTESIAN_POINT('Ctrl Pts',(-19.4975019250372,-21.5169398148659,
19.03220113298));
#214905=CARTESIAN_POINT('Ctrl Pts',(-21.3039775855559,-19.6983689841434,
19.1593769396615));
#214906=CARTESIAN_POINT('Ctrl Pts',(-20.7526583224132,-17.1950509287168,
19.2865527463429));
#214907=CARTESIAN_POINT('Ctrl Pts',(-18.3493453399679,-16.3036246104209,
19.4137285530243));
#214908=CARTESIAN_POINT('Ctrl Pts',(-16.2989291348091,-17.8419183107137,
19.5409043597057));
#214909=CARTESIAN_POINT('Ctrl Pts',(-16.4825393088626,-20.3986431089516,
19.6680801663872));
#214910=CARTESIAN_POINT('Ctrl Pts',(-18.7317249295881,-21.6281625520724,
19.7952559730686));
#214911=CARTESIAN_POINT('Ctrl Pts',(-20.9829977785724,-20.402469131249,
19.9224317797501));
#214912=CARTESIAN_POINT('Ctrl Pts',(-21.1709547689763,-17.8460599692811,
20.0496075864315));
#214913=CARTESIAN_POINT('Ctrl Pts',(-19.1231569849638,-16.3042827972216,
20.1767833931129));
#214914=CARTESIAN_POINT('Ctrl Pts',(-16.7183318756798,-17.191620562574,
20.3039591997943));
#214915=CARTESIAN_POINT('Ctrl Pts',(-16.1627570587368,-19.6939996284889,
20.4311350064758));
#214916=CARTESIAN_POINT('Ctrl Pts',(-17.9661382538539,-21.5156354105067,
20.5583108131572));
#214917=CARTESIAN_POINT('Ctrl Pts',(-20.4739845514727,-20.9853038346024,
20.6854866198387));
#214918=CARTESIAN_POINT('Ctrl Pts',(-21.3855037715295,-18.5895248239564,
20.8126624265201));
#214919=CARTESIAN_POINT('Ctrl Pts',(-19.8644314016694,-16.5263277520078,
20.9398382332015));
#214920=CARTESIAN_POINT('Ctrl Pts',(-17.3062611778333,-16.6884699406521,
21.067014039883));
#214921=CARTESIAN_POINT('Ctrl Pts',(-16.0579473234008,-18.9273846894854,
21.1941898465644));
#214922=CARTESIAN_POINT('Ctrl Pts',(-17.2647560806485,-21.1886431148375,
21.3213656532458));
#214923=CARTESIAN_POINT('Ctrl Pts',(-19.8194849413283,-21.3983814848332,
21.4485414599273));
#214924=CARTESIAN_POINT('Ctrl Pts',(-21.3783873758939,-19.3628277961746,
21.5757172666087));
#214925=CARTESIAN_POINT('Ctrl Pts',(-20.5111531531137,-16.9520807626706,
21.7028930732902));
#214926=CARTESIAN_POINT('Ctrl Pts',(-18.0136452314969,-16.3728012940309,
21.8300688799716));
#214927=CARTESIAN_POINT('Ctrl Pts',(-16.1763689660104,-18.1667340430625,
21.9572633429927));
#214928=CARTESIAN_POINT('Ctrl Pts',(-16.5172187855734,-19.8331819102065,
22.0420658704533));
#214929=CARTESIAN_POINT('Ctrl Pts',(-17.0028271735668,-20.4098093075325,
22.0844764623534));
#214930=CARTESIAN_POINT('Ctrl Pts',(-19.2802416597141,-20.9933733729761,
-0.257964067486649));
#214931=CARTESIAN_POINT('Ctrl Pts',(-19.9599077040175,-20.8115046795727,
-0.215572131926171));
#214932=CARTESIAN_POINT('Ctrl Pts',(-21.1114426467799,-19.7184754707294,
-0.130788260805215));
#214933=CARTESIAN_POINT('Ctrl Pts',(-20.6647168313355,-17.3632029388733,
-0.00361245412378029));
#214934=CARTESIAN_POINT('Ctrl Pts',(-18.4433885306129,-16.4708798215613,
0.123563352557654));
#214935=CARTESIAN_POINT('Ctrl Pts',(-16.4903434967449,-17.8521961917666,
0.250739159239088));
#214936=CARTESIAN_POINT('Ctrl Pts',(-16.5948541842955,-20.2438677216565,
0.377914965920522));
#214937=CARTESIAN_POINT('Ctrl Pts',(-18.6623442009214,-21.4496298079404,
0.505090772601956));
#214938=CARTESIAN_POINT('Ctrl Pts',(-20.7953426306735,-20.3643352377974,
0.632266579283392));
#214939=CARTESIAN_POINT('Ctrl Pts',(-21.0373071996992,-17.9831220108,0.759442385964825));
#214940=CARTESIAN_POINT('Ctrl Pts',(-19.1660680589383,-16.4908921587843,
0.886618192646261));
#214941=CARTESIAN_POINT('Ctrl Pts',(-16.8984656329369,-17.2565251572569,
1.0137939993277));
#214942=CARTESIAN_POINT('Ctrl Pts',(-16.3148352767375,-19.5776774778398,
1.14096980600913));
#214943=CARTESIAN_POINT('Ctrl Pts',(-17.9506471159836,-21.3247958511667,
1.26814561269057));
#214944=CARTESIAN_POINT('Ctrl Pts',(-20.3051320841986,-20.8950284114407,
1.395321419372));
#214945=CARTESIAN_POINT('Ctrl Pts',(-21.2182032274825,-18.6826493129518,
1.52249722605343));
#214946=CARTESIAN_POINT('Ctrl Pts',(-19.8521708785292,-16.7173846668031,
1.64967303273487));
#214947=CARTESIAN_POINT('Ctrl Pts',(-17.4602867822325,-16.8022398991988,
1.7768488394163));
#214948=CARTESIAN_POINT('Ctrl Pts',(-16.2369551795592,-18.8593671107158,
1.90402464609774));
#214949=CARTESIAN_POINT('Ctrl Pts',(-17.3045073858597,-21.0014789809986,
2.03120045277917));
#214950=CARTESIAN_POINT('Ctrl Pts',(-19.6835302529274,-21.2633212301712,
2.15837625946061));
#214951=CARTESIAN_POINT('Ctrl Pts',(-21.1914180933035,-19.4046696353217,
2.28555206614204));
#214952=CARTESIAN_POINT('Ctrl Pts',(-20.4447773338319,-17.1307217833394,
2.41272787282348));
#214953=CARTESIAN_POINT('Ctrl Pts',(-18.1286045657439,-16.5276836344422,
2.53990367950491));
#214954=CARTESIAN_POINT('Ctrl Pts',(-16.3678445270935,-18.1488052909833,
2.66707948618633));
#214955=CARTESIAN_POINT('Ctrl Pts',(-16.7778852779924,-20.5068082359283,
2.79425529286778));
#214956=CARTESIAN_POINT('Ctrl Pts',(-18.9825398744333,-21.4383711294077,
2.92143109954921));
#214957=CARTESIAN_POINT('Ctrl Pts',(-20.9591745631026,-20.0888428318423,
3.04860690623065));
#214958=CARTESIAN_POINT('Ctrl Pts',(-20.8943496995691,-17.6963317972172,
3.17578271291207));
#214959=CARTESIAN_POINT('Ctrl Pts',(-18.847538073347,-16.4558184027074,
3.30295851959352));
#214960=CARTESIAN_POINT('Ctrl Pts',(-16.6965623116711,-17.5053966934078,
3.43013432627495));
#214961=CARTESIAN_POINT('Ctrl Pts',(-16.4148091714573,-19.8821437314771,
3.55731013295638));
#214962=CARTESIAN_POINT('Ctrl Pts',(-18.2607696711808,-21.4055416272001,
3.68448593963782));
#214963=CARTESIAN_POINT('Ctrl Pts',(-20.5408896256266,-20.6779673639072,
3.81166174631925));
#214964=CARTESIAN_POINT('Ctrl Pts',(-21.163300496769,-18.3669251698599,
3.93883755300069));
#214965=CARTESIAN_POINT('Ctrl Pts',(-19.5569789415241,-16.5926528186193,
4.06601335968212));
#214966=CARTESIAN_POINT('Ctrl Pts',(-17.1956252872621,-16.9829350686982,
4.19318916636356));
#214967=CARTESIAN_POINT('Ctrl Pts',(-16.2456349496354,-19.1797121792916,
4.32036497304499));
#214968=CARTESIAN_POINT('Ctrl Pts',(-17.5785651003642,-21.1675774987978,
4.44754077972642));
#214969=CARTESIAN_POINT('Ctrl Pts',(-19.9715350571314,-21.1227879774049,
4.57471658640786));
#214970=CARTESIAN_POINT('Ctrl Pts',(-21.2291434090686,-19.0864352210401,
4.70189239308929));
#214971=CARTESIAN_POINT('Ctrl Pts',(-20.197612549251,-16.9267464933619,
4.82906819977073));
#214972=CARTESIAN_POINT('Ctrl Pts',(-17.8233080175354,-16.6251021566151,
4.95624400645216));
#214973=CARTESIAN_POINT('Ctrl Pts',(-16.284506855812,-18.4582421676058,
5.0834198131336));
#214974=CARTESIAN_POINT('Ctrl Pts',(-16.9929636211903,-20.7443743437509,
5.21059561981502));
#214975=CARTESIAN_POINT('Ctrl Pts',(-19.298713203222,-21.3861143068026,
5.33777142649647));
#214976=CARTESIAN_POINT('Ctrl Pts',(-21.0863734713516,-19.7947054715354,
5.4649472331779));
#214977=CARTESIAN_POINT('Ctrl Pts',(-20.7158770842802,-17.4301666703347,
5.59212303985933));
#214978=CARTESIAN_POINT('Ctrl Pts',(-18.5271314815462,-16.4618154934729,
5.71929884654077));
#214979=CARTESIAN_POINT('Ctrl Pts',(-16.5281749047854,-17.7780540430683,
5.8464746532222));
#214980=CARTESIAN_POINT('Ctrl Pts',(-16.552925943938,-20.171315144845,5.97365045990364));
#214981=CARTESIAN_POINT('Ctrl Pts',(-18.5786770568045,-21.4459302804593,
6.10082626658507));
#214982=CARTESIAN_POINT('Ctrl Pts',(-20.7469273296236,-20.4325191745226,
6.22800207326651));
#214983=CARTESIAN_POINT('Ctrl Pts',(-21.0684417138734,-18.0608236173447,
6.35517787994794));
#214984=CARTESIAN_POINT('Ctrl Pts',(-19.2482507174378,-16.5067270786087,
6.48235368662938));
#214985=CARTESIAN_POINT('Ctrl Pts',(-16.9562666057522,-17.1960166744951,
6.6095294933108));
#214986=CARTESIAN_POINT('Ctrl Pts',(-16.2952425447106,-19.4963119829154,
6.73670529999224));
#214987=CARTESIAN_POINT('Ctrl Pts',(-17.8716270825383,-21.2972348308226,
6.86388110667369));
#214988=CARTESIAN_POINT('Ctrl Pts',(-20.2391852472374,-20.94655028314,6.9910569133551));
#214989=CARTESIAN_POINT('Ctrl Pts',(-21.2258293699287,-18.7659896464285,
7.11823272003656));
#214990=CARTESIAN_POINT('Ctrl Pts',(-19.9263747060834,-16.7560819640143,
7.24540852671797));
#214991=CARTESIAN_POINT('Ctrl Pts',(-17.5329902565274,-16.7607927855726,
7.37258433339943));
#214992=CARTESIAN_POINT('Ctrl Pts',(-16.2414577035358,-18.7758002247102,
7.49976014008084));
#214993=CARTESIAN_POINT('Ctrl Pts',(-17.2366780029277,-20.9524600214847,
7.62693594676229));
#214994=CARTESIAN_POINT('Ctrl Pts',(-19.6055983003493,-21.293821911099,
7.75411175344372));
#214995=CARTESIAN_POINT('Ctrl Pts',(-21.1748812546918,-19.48670754714,7.88128756012516));
#214996=CARTESIAN_POINT('Ctrl Pts',(-20.5048071560311,-17.1890321963735,
8.00846336680658));
#214997=CARTESIAN_POINT('Ctrl Pts',(-18.2101274003992,-16.5087703833118,
8.13563917348801));
#214998=CARTESIAN_POINT('Ctrl Pts',(-16.3960682397005,-18.0700200996293,
8.26281498016946));
#214999=CARTESIAN_POINT('Ctrl Pts',(-16.7269163606663,-20.4404316326905,
8.38999078685089));
#215000=CARTESIAN_POINT('Ctrl Pts',(-18.8991391470608,-21.4452995252443,
8.51716659353233));
#215001=CARTESIAN_POINT('Ctrl Pts',(-20.9198570157183,-20.1627198550076,
8.64434240021374));
#215002=CARTESIAN_POINT('Ctrl Pts',(-20.9351867420414,-17.7693798635505,
8.77151820689519));
#215003=CARTESIAN_POINT('Ctrl Pts',(-18.9310642535986,-16.4610204456021,
8.89869401357662));
#215004=CARTESIAN_POINT('Ctrl Pts',(-16.7461475436661,-17.4379801611861,
9.02586982025806));
#215005=CARTESIAN_POINT('Ctrl Pts',(-16.3849620823817,-19.8039591082128,
9.15304562693949));
#215006=CARTESIAN_POINT('Ctrl Pts',(-18.1788731127761,-21.3883184520001,
9.28022143362092));
#215007=CARTESIAN_POINT('Ctrl Pts',(-20.4820786071378,-20.7375068310543,
9.40739724030236));
#215008=CARTESIAN_POINT('Ctrl Pts',(-21.1815304774453,-18.4486035136685,
9.53457304698381));
#215009=CARTESIAN_POINT('Ctrl Pts',(-19.6355250455705,-16.6215352281822,
9.66174885366522));
#215010=CARTESIAN_POINT('Ctrl Pts',(-17.2624263393396,-16.932523725882,
9.78892466034668));
#215011=CARTESIAN_POINT('Ctrl Pts',(-16.2394051306023,-19.0962563622516,
9.91610046702808));
#215012=CARTESIAN_POINT('Ctrl Pts',(-17.5050198825181,-21.1276427398149,
10.0432762737096));
#215013=CARTESIAN_POINT('Ctrl Pts',(-19.8981476131147,-21.1630119392157,
10.170452080391));
#215014=CARTESIAN_POINT('Ctrl Pts',(-21.2232421638282,-19.1699149152638,
10.2976278870724));
#215015=CARTESIAN_POINT('Ctrl Pts',(-20.2646115290223,-16.9768944818824,
10.4248036937539));
#215016=CARTESIAN_POINT('Ctrl Pts',(-17.901739816804,-16.5959107725,10.5519795004353));
#215017=CARTESIAN_POINT('Ctrl Pts',(-16.3024151667752,-18.3764926939591,
10.6791553071167));
#215018=CARTESIAN_POINT('Ctrl Pts',(-16.9339186800547,-20.6850668486988,
10.8063311137982));
#215019=CARTESIAN_POINT('Ctrl Pts',(-19.2168850787369,-21.4036597360172,
10.9335069204796));
#215020=CARTESIAN_POINT('Ctrl Pts',(-21.0568343889061,-19.8730069827043,
11.0606827271611));
#215021=CARTESIAN_POINT('Ctrl Pts',(-20.7657273186155,-17.4973874869004,
11.1878585338425));
#215022=CARTESIAN_POINT('Ctrl Pts',(-18.6106365367144,-16.4562846884308,
11.3150343405239));
#215023=CARTESIAN_POINT('Ctrl Pts',(-16.5687240755777,-17.7048457867641,
11.4422101472054));
#215024=CARTESIAN_POINT('Ctrl Pts',(-16.5133178829179,-20.0975934686209,
11.5693859538868));
#215025=CARTESIAN_POINT('Ctrl Pts',(-18.4952497016042,-21.4393302465677,
11.6965617605682));
#215026=CARTESIAN_POINT('Ctrl Pts',(-20.6962201005539,-20.4990959044147,
11.8237375672497));
#215027=CARTESIAN_POINT('Ctrl Pts',(-21.09697534636,-18.1394970935624,11.9509133739311));
#215028=CARTESIAN_POINT('Ctrl Pts',(-19.3298473746713,-16.5253192697488,
12.0780891806125));
#215029=CARTESIAN_POINT('Ctrl Pts',(-17.0160664191804,-17.1374703991481,
12.205264987294));
#215030=CARTESIAN_POINT('Ctrl Pts',(-16.2783828971083,-19.4143398149205,
12.3324407939754));
#215031=CARTESIAN_POINT('Ctrl Pts',(-17.7935756541529,-21.2670411465485,
12.4596166006568));
#215032=CARTESIAN_POINT('Ctrl Pts',(-20.1715493791944,-20.9958359138768,
12.5867924073383));
#215033=CARTESIAN_POINT('Ctrl Pts',(-21.2306607732021,-18.8495380849864,
12.7139682140197));
#215034=CARTESIAN_POINT('Ctrl Pts',(-19.9992408680408,-16.7972427036174,
12.8411440207011));
#215035=CARTESIAN_POINT('Ctrl Pts',(-17.6070409961567,-16.7218034023586,
12.9683198273826));
#215036=CARTESIAN_POINT('Ctrl Pts',(-16.2487560633345,-18.6924310578239,
13.095495634064));
#215037=CARTESIAN_POINT('Ctrl Pts',(-17.1705281907678,-20.9011971070702,
13.2226714407454));
#215038=CARTESIAN_POINT('Ctrl Pts',(-19.526688663167,-21.3216957913963,
13.3498472474269));
#215039=CARTESIAN_POINT('Ctrl Pts',(-21.1556064869176,-19.5681456670245,
13.4770230541083));
#215040=CARTESIAN_POINT('Ctrl Pts',(-20.5628506607707,-17.2493201354707,
13.6041988607897));
#215041=CARTESIAN_POINT('Ctrl Pts',(-18.2922378646403,-16.4925976993917,
13.7313746674712));
#215042=CARTESIAN_POINT('Ctrl Pts',(-16.426914408852,-17.9922242263985,
13.8585504741526));
#215043=CARTESIAN_POINT('Ctrl Pts',(-16.6781987890609,-20.3723854552819,
13.985726280834));
#215044=CARTESIAN_POINT('Ctrl Pts',(-18.8155531828929,-21.449431188008,
14.1129020875155));
#215045=CARTESIAN_POINT('Ctrl Pts',(-20.878087593182,-20.2352388137978,
14.2400778941968));
#215046=CARTESIAN_POINT('Ctrl Pts',(-20.973554713811,-17.8437544747116,
14.3672537008784));
#215047=CARTESIAN_POINT('Ctrl Pts',(-19.0143693869603,-16.4690166196025,
14.4944295075598));
#215048=CARTESIAN_POINT('Ctrl Pts',(-16.7979625492603,-17.372261904679,
14.6216053142412));
#215049=CARTESIAN_POINT('Ctrl Pts',(-16.3577499085777,-19.7248188426085,
14.7487811209226));
#215050=CARTESIAN_POINT('Ctrl Pts',(-18.097599240061,-21.3683624589916,
14.8759569276041));
#215051=CARTESIAN_POINT('Ctrl Pts',(-20.4213067693024,-20.7950434956184,
15.0031327342855));
#215052=CARTESIAN_POINT('Ctrl Pts',(-21.1970150637779,-18.5308465171956,
15.130308540967));
#215053=CARTESIAN_POINT('Ctrl Pts',(-19.7130599091926,-16.6530317195128,
15.2574843476484));
#215054=CARTESIAN_POINT('Ctrl Pts',(-17.3308780552345,-16.884377629113,
15.3846601543298));
#215055=CARTESIAN_POINT('Ctrl Pts',(-16.2359734980291,-19.0126387328847,
15.5118359610112));
#215056=CARTESIAN_POINT('Ctrl Pts',(-17.4328532113714,-21.0852675628988,
15.6390117676927));
#215057=CARTESIAN_POINT('Ctrl Pts',(-19.823454345003,-21.2007558094709,
15.7661875743741));
#215058=CARTESIAN_POINT('Ctrl Pts',(-21.2145487362569,-19.2531501743798,
15.8933633810556));
#215059=CARTESIAN_POINT('Ctrl Pts',(-20.3298936222131,-17.0292579457831,
16.020539187737));
#215060=CARTESIAN_POINT('Ctrl Pts',(-17.9811051621181,-16.5693622130996,
16.1477149944184));
#215061=CARTESIAN_POINT('Ctrl Pts',(-16.3230509858558,-18.295388766718,
16.2748908010999));
#215062=CARTESIAN_POINT('Ctrl Pts',(-16.8768928896987,-20.6238153729833,
16.4020666077813));
#215063=CARTESIAN_POINT('Ctrl Pts',(-19.1345153021762,-21.418455139101,
16.5292424144627));
#215064=CARTESIAN_POINT('Ctrl Pts',(-21.0246897836904,-19.9502754005642,
16.6564182211442));
#215065=CARTESIAN_POINT('Ctrl Pts',(-20.8132985649108,-17.5662399419689,
16.7835940278256));
#215066=CARTESIAN_POINT('Ctrl Pts',(-18.6942799686495,-16.4535533266478,
16.910769834507));
#215067=CARTESIAN_POINT('Ctrl Pts',(-16.6117020358488,-17.6330364630381,
17.0379456411885));
#215068=CARTESIAN_POINT('Ctrl Pts',(-16.4762007604896,-20.0225867804811,
17.1651214478699));
#215069=CARTESIAN_POINT('Ctrl Pts',(-18.4120901525558,-21.4299401749425,
17.2922972545513));
#215070=CARTESIAN_POINT('Ctrl Pts',(-20.6433118496738,-20.563937257206,
17.4194730612328));
#215071=CARTESIAN_POINT('Ctrl Pts',(-21.1228584299742,-18.2190819540937,
17.5466488679142));
#215072=CARTESIAN_POINT('Ctrl Pts',(-19.4107756700491,-16.5466334680738,
17.6738246745956));
#215073=CARTESIAN_POINT('Ctrl Pts',(-17.0777932382892,-17.0809594812165,
17.8010004812771));
#215074=CARTESIAN_POINT('Ctrl Pts',(-16.2642777146144,-19.3318490404626,
17.9281762879585));
#215075=CARTESIAN_POINT('Ctrl Pts',(-17.7165790995274,-21.2342506811916,
18.05535209464));
#215076=CARTESIAN_POINT('Ctrl Pts',(-20.1023010123624,-21.0428289743473,
18.1825279013214));
#215077=CARTESIAN_POINT('Ctrl Pts',(-21.2326916726909,-18.9332014550839,
18.3097037080028));
#215078=CARTESIAN_POINT('Ctrl Pts',(-20.0706878096263,-16.8408204338905,
18.4368795146842));
#215079=CARTESIAN_POINT('Ctrl Pts',(-17.6823558454215,-16.6853156302542,
18.5640553213657));
#215080=CARTESIAN_POINT('Ctrl Pts',(-16.2588421206643,-18.6093530491115,
18.6912311280471));
#215081=CARTESIAN_POINT('Ctrl Pts',(-17.1061321245363,-20.8477477792071,
18.8184069347286));
#215082=CARTESIAN_POINT('Ctrl Pts',(-19.4468898673433,-21.3469115835881,
18.94558274141));
#215083=CARTESIAN_POINT('Ctrl Pts',(-21.1336154036588,-19.6488926582199,
19.0727585480914));
#215084=CARTESIAN_POINT('Ctrl Pts',(-20.6188427443147,-17.3115179667752,
19.1999343547728));
#215085=CARTESIAN_POINT('Ctrl Pts',(-18.3748438530787,-16.4791837329545,
19.3271101614543));
#215086=CARTESIAN_POINT('Ctrl Pts',(-16.4603484358955,-17.9155049208591,
19.4542859681357));
#215087=CARTESIAN_POINT('Ctrl Pts',(-16.6317872081259,-20.302746056054,
19.5814617748171));
#215088=CARTESIAN_POINT('Ctrl Pts',(-18.7318757425608,-21.4507614361853,
19.7086375814986));
#215089=CARTESIAN_POINT('Ctrl Pts',(-20.8339131442188,-20.3063184537634,
19.83581338818));
#215090=CARTESIAN_POINT('Ctrl Pts',(-21.0094105851045,-17.9193720315106,
19.9629891948615));
#215091=CARTESIAN_POINT('Ctrl Pts',(-19.0973600155928,-16.4797982889704,
20.0901650015429));
#215092=CARTESIAN_POINT('Ctrl Pts',(-16.8519492354458,-17.3083149974252,
20.2173408082243));
#215093=CARTESIAN_POINT('Ctrl Pts',(-16.3332031202602,-19.6448129443766,
20.3445166149058));
#215094=CARTESIAN_POINT('Ctrl Pts',(-18.01703932132,-21.3456936473654,20.4716924215872));
#215095=CARTESIAN_POINT('Ctrl Pts',(-20.358642080658,-20.8505174148026,
20.5988682282686));
#215096=CARTESIAN_POINT('Ctrl Pts',(-21.2097372705433,-18.6135530731602,
20.72604403495));
#215097=CARTESIAN_POINT('Ctrl Pts',(-19.7894958220145,-16.6871240247294,
20.8532198416315));
#215098=CARTESIAN_POINT('Ctrl Pts',(-17.4009050775665,-16.8385179106685,
20.9803956483129));
#215099=CARTESIAN_POINT('Ctrl Pts',(-16.2353411557127,-18.9290164227857,
21.1075714549944));
#215100=CARTESIAN_POINT('Ctrl Pts',(-17.3621513269132,-21.0403774632962,
21.2347472616758));
#215101=CARTESIAN_POINT('Ctrl Pts',(-19.7475288339831,-21.2362124099542,
21.3619230683572));
#215102=CARTESIAN_POINT('Ctrl Pts',(-21.2030926162545,-19.335594282492,
21.4890988750387));
#215103=CARTESIAN_POINT('Ctrl Pts',(-20.3933467993028,-17.0846541387204,
21.6162746817201));
#215104=CARTESIAN_POINT('Ctrl Pts',(-18.0613970915878,-16.5437747381437,
21.7434504884015));
#215105=CARTESIAN_POINT('Ctrl Pts',(-16.3459127028459,-18.2187888246082,
21.8706449514226));
#215106=CARTESIAN_POINT('Ctrl Pts',(-16.6641678043512,-19.7747689210369,
21.9554474788832));
#215107=CARTESIAN_POINT('Ctrl Pts',(-17.117585520725,-20.3131720544228,
21.9978580707833));
#215108=CARTESIAN_POINT('Ctrl Pts',(-19.3957372685685,-21.4249949024184,
-1.39254927034038E-15));
#215109=CARTESIAN_POINT('Ctrl Pts',(-19.4773891020297,-21.3954306668132,
2.38531586308131E-15));
#215110=CARTESIAN_POINT('Ctrl Pts',(-19.5571492231821,-21.3614659991419,
1.6186890260879E-14));
#215111=CARTESIAN_POINT('Ctrl Pts',(-19.6348156046203,-21.3234187284543,
1.5709655798446E-14));
#215112=CARTESIAN_POINT('Ctrl Pts',(-19.7143272588109,-21.2844674940362,
1.5221082739651E-14));
#215113=CARTESIAN_POINT('Ctrl Pts',(-19.791645221544,-21.2412367046751,
5.31486745776737E-15));
#215114=CARTESIAN_POINT('Ctrl Pts',(-19.8665232792529,-21.1940209467401,
3.51454976232901E-15));
#215115=CARTESIAN_POINT('Ctrl Pts',(-19.9365886939553,-21.1498398907482,
1.82994402085299E-15));
#215116=CARTESIAN_POINT('Ctrl Pts',(-20.0045179028409,-21.1021686855581,
2.13733777873822E-15));
#215117=CARTESIAN_POINT('Ctrl Pts',(-20.0700783470716,-21.0512211850772,
-1.82284742855643E-14));
#215118=CARTESIAN_POINT('Ctrl Pts',(-20.0997467345518,-21.0281656642803,
-2.7297595720857E-14));
#215119=CARTESIAN_POINT('Ctrl Pts',(-20.128929580841,-21.0044388940273,
8.44227451794598E-16));
#215120=CARTESIAN_POINT('Ctrl Pts',(-20.1576029444589,-20.9800594108908,
2.3037127760972E-15));
#215121=CARTESIAN_POINT('Ctrl Pts',(-20.1753081557669,-20.9650055823179,
2.84180167051755E-15));
#215122=CARTESIAN_POINT('Ctrl Pts',(-20.1928190804462,-20.9497028729833,
-1.45985713076056E-14));
#215123=CARTESIAN_POINT('Ctrl Pts',(-20.2101297684373,-20.9341555341053,
-1.7874590696465E-14));
#215124=CARTESIAN_POINT('Ctrl Pts',(-20.2222918053998,-20.923232380144,
-1.99659078843905E-14));
#215125=CARTESIAN_POINT('Ctrl Pts',(-20.2343567785502,-20.9121866751007,
-2.1053807985098E-14));
#215126=CARTESIAN_POINT('Ctrl Pts',(-20.2463057260566,-20.9010359825867,
-1.90333859784175E-14));
#215127=CARTESIAN_POINT('Ctrl Pts',(-20.3097375112913,-20.8418417872492,
-8.05854395286965E-15));
#215128=CARTESIAN_POINT('Ctrl Pts',(-20.3700069578684,-20.7796002467127,
-1.58672311013317E-14));
#215129=CARTESIAN_POINT('Ctrl Pts',(-20.4268835059678,-20.7145895545046,
-1.55431223447522E-15));
#215130=CARTESIAN_POINT('Ctrl Pts',(-20.4830376461208,-20.6504045847113,
1.25768134914526E-14));
#215131=CARTESIAN_POINT('Ctrl Pts',(-20.5358849804778,-20.583519523084,
-3.34795984228788E-14));
#215132=CARTESIAN_POINT('Ctrl Pts',(-20.5851611052647,-20.5141759583156,
-1.8471335572201E-14));
#215133=CARTESIAN_POINT('Ctrl Pts',(-20.6305983443516,-20.4502346450498,
-4.63230033198983E-15));
#215134=CARTESIAN_POINT('Ctrl Pts',(-20.6729990002168,-20.3842022514996,
-1.1961046526289E-14));
#215135=CARTESIAN_POINT('Ctrl Pts',(-20.7121180817081,-20.3162569684087,
-1.55292445569444E-14));
#215136=CARTESIAN_POINT('Ctrl Pts',(-20.7284901400346,-20.2878206121505,
-1.7251812553125E-14));
#215137=CARTESIAN_POINT('Ctrl Pts',(-20.7442869378835,-20.2590491139325,
-1.72679665432114E-15));
#215138=CARTESIAN_POINT('Ctrl Pts',(-20.7594884026036,-20.2299553026624,
8.32667268468867E-16));
#215139=CARTESIAN_POINT('Ctrl Pts',(-20.7693451022676,-20.2110907415789,
2.84488477332053E-15));
#215140=CARTESIAN_POINT('Ctrl Pts',(-20.7789514808442,-20.1920906691223,
-5.33029635918034E-15));
#215141=CARTESIAN_POINT('Ctrl Pts',(-20.7883017662921,-20.1729585792041,
-1.32671651442706E-14));
#215142=CARTESIAN_POINT('Ctrl Pts',(-20.7942277139279,-20.1608331993265,
-1.8152373887588E-14));
#215143=CARTESIAN_POINT('Ctrl Pts',(-20.8000469683619,-20.1486625665028,
1.84527092251997E-14));
#215144=CARTESIAN_POINT('Ctrl Pts',(-20.8057568610096,-20.1364512427194,
1.4585554986013E-14));
#215145=CARTESIAN_POINT('Ctrl Pts',(-20.8408823973353,-20.0613308641761,
-8.46139807618924E-15));
#215146=CARTESIAN_POINT('Ctrl Pts',(-20.8718944952827,-19.9846287385395,
1.40630333927033E-15));
#215147=CARTESIAN_POINT('Ctrl Pts',(-20.8985463569486,-19.9065734343537,
-7.97972798949331E-15));
#215148=CARTESIAN_POINT('Ctrl Pts',(-20.9251982186144,-19.8285181301678,
-1.7094606859296E-14));
#215149=CARTESIAN_POINT('Ctrl Pts',(-20.9474903161071,-19.7491089176507,
-2.28260845907407E-14));
#215150=CARTESIAN_POINT('Ctrl Pts',(-20.9651215428786,-19.6685651028304,
-1.17128529097954E-14));
#215151=CARTESIAN_POINT('Ctrl Pts',(-20.9829460124324,-19.5871385070737,
-3.41913440983829E-16));
#215152=CARTESIAN_POINT('Ctrl Pts',(-20.9960061448808,-19.5045510760419,
-8.44412583292002E-15));
#215153=CARTESIAN_POINT('Ctrl Pts',(-21.0043775994437,-19.4211942605515,
-5.21804821573824E-15));
#215154=CARTESIAN_POINT('Ctrl Pts',(-21.0078360662703,-19.3867573799617,
-3.86087694338245E-15));
#215155=CARTESIAN_POINT('Ctrl Pts',(-21.0104937056419,-19.3521893421996,
6.81493208789715E-15));
#215156=CARTESIAN_POINT('Ctrl Pts',(-21.0123534306943,-19.3175186761032,
9.90874049477952E-15));
#215157=CARTESIAN_POINT('Ctrl Pts',(-21.0130853886539,-19.3038728578793,
1.11360150531808E-14));
#215158=CARTESIAN_POINT('Ctrl Pts',(-21.0136937288726,-19.2902091507495,
9.61300125740955E-15));
#215159=CARTESIAN_POINT('Ctrl Pts',(-21.0141781582269,-19.2765469516024,
8.43769498715119E-15));
#215160=CARTESIAN_POINT('Ctrl Pts',(-21.0170629175674,-19.1951890482203,
-2.3977240746094E-16));
#215161=CARTESIAN_POINT('Ctrl Pts',(-21.0155663596031,-19.1137544906502,
3.90840785478979E-15));
#215162=CARTESIAN_POINT('Ctrl Pts',(-21.0098211098971,-19.032600466024,
6.68909372336657E-15));
#215163=CARTESIAN_POINT('Ctrl Pts',(-21.0040551996082,-18.9511546021311,
9.47977926020773E-15));
#215164=CARTESIAN_POINT('Ctrl Pts',(-20.9940096109013,-18.8699902747437,
4.03215545607249E-16));
#215165=CARTESIAN_POINT('Ctrl Pts',(-20.9797677234132,-18.7894801122668,
9.35362898246694E-15));
#215166=CARTESIAN_POINT('Ctrl Pts',(-20.9656475490767,-18.709658000838,
1.82275509410235E-14));
#215167=CARTESIAN_POINT('Ctrl Pts',(-20.9474020559152,-18.6304779977789,
-4.3520267587977E-15));
#215168=CARTESIAN_POINT('Ctrl Pts',(-20.9250689772833,-18.5523290403031,
-3.21964677141295E-15));
#215169=CARTESIAN_POINT('Ctrl Pts',(-20.9157717581042,-18.5197957743688,
-2.81628118295938E-15));
#215170=CARTESIAN_POINT('Ctrl Pts',(-20.9057656579654,-18.487441581366,
8.12354228918885E-15));
#215171=CARTESIAN_POINT('Ctrl Pts',(-20.895051417118,-18.4552964308102,
-9.57567358739198E-15));
#215172=CARTESIAN_POINT('Ctrl Pts',(-20.8895107429844,-18.4386731528066,
-1.88289619471796E-14));
#215173=CARTESIAN_POINT('Ctrl Pts',(-20.8837798116562,-18.4221037461655,
-4.83972879403747E-15));
#215174=CARTESIAN_POINT('Ctrl Pts',(-20.8778666087312,-18.4056137222238,
-3.13638004456607E-15));
#215175=CARTESIAN_POINT('Ctrl Pts',(-20.8511334397242,-18.3310634991803,
4.89831143352979E-15));
#215176=CARTESIAN_POINT('Ctrl Pts',(-20.820647395102,-18.2580374311815,
-9.744766559422E-15));
#215177=CARTESIAN_POINT('Ctrl Pts',(-20.7864673279414,-18.1868947789178,
-2.66453525910038E-15));
#215178=CARTESIAN_POINT('Ctrl Pts',(-20.7601551114488,-18.132128330993,
2.78590981802746E-15));
#215179=CARTESIAN_POINT('Ctrl Pts',(-20.7316528702852,-18.0784783891692,
2.11663013799853E-15));
#215180=CARTESIAN_POINT('Ctrl Pts',(-20.7009722503935,-18.0261235328628,
1.55986334959834E-14));
#215181=CARTESIAN_POINT('Ctrl Pts',(-20.6917379810896,-18.0103657403473,
1.97460531307573E-14));
#215182=CARTESIAN_POINT('Ctrl Pts',(-20.6823062897647,-17.9947253717853,
1.79594778764635E-14));
#215183=CARTESIAN_POINT('Ctrl Pts',(-20.6726772825947,-17.9792075775192,
1.94289029309402E-14));
#215184=CARTESIAN_POINT('Ctrl Pts',(-20.6644523726372,-17.9659525805787,
2.06523250739444E-14));
#215185=CARTESIAN_POINT('Ctrl Pts',(-20.6560857633015,-17.9527907829532,
9.64787106585675E-16));
#215186=CARTESIAN_POINT('Ctrl Pts',(-20.6475820647203,-17.939731697129,
8.60422844084496E-16));
#215187=CARTESIAN_POINT('Ctrl Pts',(-20.6064305493276,-17.8765355282888,
2.51002288245022E-16));
#215188=CARTESIAN_POINT('Ctrl Pts',(-20.5620419163801,-17.8156943120763,
1.53373012318955E-14));
#215189=CARTESIAN_POINT('Ctrl Pts',(-20.5144495416444,-17.7575477797155,
1.39610545346613E-14));
#215190=CARTESIAN_POINT('Ctrl Pts',(-20.4703172832204,-17.7036286843383,
1.22109826709272E-14));
#215191=CARTESIAN_POINT('Ctrl Pts',(-20.4234296462928,-17.6520265735113,
-9.73370719758813E-15));
#215192=CARTESIAN_POINT('Ctrl Pts',(-20.3737906735959,-17.6030455128839,
-2.54796184151473E-14));
#215193=CARTESIAN_POINT('Ctrl Pts',(-20.368202112649,-17.5975310224002,
-2.7237392166664E-14));
#215194=CARTESIAN_POINT('Ctrl Pts',(-20.3625786573857,-17.5920497923538,
-1.59933772775865E-15));
#215195=CARTESIAN_POINT('Ctrl Pts',(-20.3569206763285,-17.5866019717796,
2.66453525910038E-15));
#215196=CARTESIAN_POINT('Origin',(23.734,9.62950000000001,14.8));
#215197=CARTESIAN_POINT('',(23.734,10.6295,14.8));
#215198=CARTESIAN_POINT('',(23.734,9.62950000000001,14.8));
#215199=CARTESIAN_POINT('',(23.734,14.42025,14.8));
#215200=CARTESIAN_POINT('',(23.534,9.62950000000001,14.8));
#215201=CARTESIAN_POINT('',(23.734,9.62950000000001,14.8));
#215202=CARTESIAN_POINT('',(23.534,10.6295,14.8));
#215203=CARTESIAN_POINT('',(23.534,10.6295,14.8));
#215204=CARTESIAN_POINT('',(23.734,10.6295,14.8));
#215205=CARTESIAN_POINT('Origin',(23.734,9.62950000000001,17.2));
#215206=CARTESIAN_POINT('',(23.734,9.62950000000001,17.2));
#215207=CARTESIAN_POINT('',(23.734,9.62950000000001,8.6));
#215208=CARTESIAN_POINT('',(23.534,9.62950000000001,17.2));
#215209=CARTESIAN_POINT('',(23.734,9.62950000000001,17.2));
#215210=CARTESIAN_POINT('',(23.534,9.62950000000001,14.8));
#215211=CARTESIAN_POINT('Origin',(23.734,9.12950000000001,17.2));
#215212=CARTESIAN_POINT('',(23.734,9.12950000000001,17.2));
#215213=CARTESIAN_POINT('',(23.734,14.17025,17.2));
#215214=CARTESIAN_POINT('',(23.534,9.12950000000001,17.2));
#215215=CARTESIAN_POINT('',(23.734,9.12950000000001,17.2));
#215216=CARTESIAN_POINT('',(23.534,9.62950000000001,17.2));
#215217=CARTESIAN_POINT('Origin',(23.734,10.1295,19.2));
#215218=CARTESIAN_POINT('',(23.734,10.1295,19.2));
#215219=CARTESIAN_POINT('',(23.734,7.19765,13.3363));
#215220=CARTESIAN_POINT('',(23.534,10.1295,19.2));
#215221=CARTESIAN_POINT('',(23.734,10.1295,19.2));
#215222=CARTESIAN_POINT('',(23.534,9.12950000000001,17.2));
#215223=CARTESIAN_POINT('Origin',(23.734,11.1295,17.2));
#215224=CARTESIAN_POINT('',(23.734,11.1295,17.2));
#215225=CARTESIAN_POINT('',(23.734,15.37765,8.7037));
#215226=CARTESIAN_POINT('',(23.534,11.1295,17.2));
#215227=CARTESIAN_POINT('',(23.734,11.1295,17.2));
#215228=CARTESIAN_POINT('',(23.534,11.1295,17.2));
#215229=CARTESIAN_POINT('Origin',(23.734,10.6295,17.2));
#215230=CARTESIAN_POINT('',(23.734,10.6295,17.2));
#215231=CARTESIAN_POINT('',(23.734,14.92025,17.2));
#215232=CARTESIAN_POINT('',(23.534,10.6295,17.2));
#215233=CARTESIAN_POINT('',(23.734,10.6295,17.2));
#215234=CARTESIAN_POINT('',(23.534,10.6295,17.2));
#215235=CARTESIAN_POINT('Origin',(23.734,10.6295,14.8));
#215236=CARTESIAN_POINT('',(23.734,10.6295,7.4));
#215237=CARTESIAN_POINT('',(23.534,10.6295,14.8));
#215238=CARTESIAN_POINT('Origin',(23.734,10.1295,17.));
#215239=CARTESIAN_POINT('',(23.734,10.1295,20.));
#215240=CARTESIAN_POINT('Origin',(23.734,10.1295,17.));
#215241=CARTESIAN_POINT('',(23.534,10.1295,20.));
#215242=CARTESIAN_POINT('',(23.734,10.1295,20.));
#215243=CARTESIAN_POINT('Origin',(23.534,10.1295,17.));
#215244=CARTESIAN_POINT('Origin',(23.534,10.1295,17.));
#215245=CARTESIAN_POINT('Origin',(23.734,-9.8705,7.));
#215246=CARTESIAN_POINT('',(23.734,-5.8705,11.4721359549996));
#215247=CARTESIAN_POINT('',(23.734,-3.8705,7.));
#215248=CARTESIAN_POINT('Origin',(23.734,-9.8705,7.));
#215249=CARTESIAN_POINT('',(23.534,-3.87049999999999,7.));
#215250=CARTESIAN_POINT('',(23.734,-3.8705,7.));
#215251=CARTESIAN_POINT('',(23.534,-5.8705,11.4721359549996));
#215252=CARTESIAN_POINT('Origin',(23.534,-9.8705,7.));
#215253=CARTESIAN_POINT('',(23.734,-5.8705,11.4721359549996));
#215254=CARTESIAN_POINT('Origin',(23.734,4.1295,7.));
#215255=CARTESIAN_POINT('',(23.734,4.1295,7.));
#215256=CARTESIAN_POINT('',(23.734,11.67025,7.));
#215257=CARTESIAN_POINT('',(23.534,4.1295,7.));
#215258=CARTESIAN_POINT('',(23.734,4.1295,7.));
#215259=CARTESIAN_POINT('',(23.534,4.1295,7.));
#215260=CARTESIAN_POINT('Origin',(23.734,10.1295,7.));
#215261=CARTESIAN_POINT('',(23.734,6.1295,11.4721359549996));
#215262=CARTESIAN_POINT('Origin',(23.734,10.1295,7.));
#215263=CARTESIAN_POINT('',(23.534,6.1295,11.4721359549996));
#215264=CARTESIAN_POINT('',(23.734,6.1295,11.4721359549996));
#215265=CARTESIAN_POINT('Origin',(23.534,10.1295,7.));
#215266=CARTESIAN_POINT('Origin',(23.734,6.1295,22.));
#215267=CARTESIAN_POINT('',(23.734,6.1295,11.));
#215268=CARTESIAN_POINT('',(23.534,6.1295,22.));
#215269=CARTESIAN_POINT('Origin',(23.734,-5.8705,11.4721359549996));
#215270=CARTESIAN_POINT('',(23.734,-5.8705,5.73606797749979));
#215271=CARTESIAN_POINT('',(23.534,-5.8705,22.));
#215272=CARTESIAN_POINT('Origin',(23.534,0.129500000000005,11.5));
#215273=CARTESIAN_POINT('',(23.534,0.129500000000002,21.));
#215274=CARTESIAN_POINT('Origin',(23.534,0.129500000000004,17.));
#215275=CARTESIAN_POINT('',(23.534,-9.8705,12.));
#215276=CARTESIAN_POINT('Origin',(23.534,-9.8705,7.));
#215277=CARTESIAN_POINT('Origin',(23.734,-9.37049999999999,16.8));
#215278=CARTESIAN_POINT('',(23.734,-9.37049999999999,19.2));
#215279=CARTESIAN_POINT('',(23.734,-9.37049999999999,16.8));
#215280=CARTESIAN_POINT('',(23.734,-9.37049999999999,8.4));
#215281=CARTESIAN_POINT('',(23.534,-9.37049999999999,16.8));
#215282=CARTESIAN_POINT('',(23.734,-9.37049999999999,16.8));
#215283=CARTESIAN_POINT('',(23.534,-9.37049999999999,19.2));
#215284=CARTESIAN_POINT('',(23.534,-9.37049999999999,19.2));
#215285=CARTESIAN_POINT('',(23.734,-9.37049999999999,19.2));
#215286=CARTESIAN_POINT('Origin',(23.734,-8.87049999999999,16.8));
#215287=CARTESIAN_POINT('',(23.734,-8.87049999999999,16.8));
#215288=CARTESIAN_POINT('',(23.734,5.17025,16.8));
#215289=CARTESIAN_POINT('',(23.534,-8.87049999999999,16.8));
#215290=CARTESIAN_POINT('',(23.734,-8.87049999999999,16.8));
#215291=CARTESIAN_POINT('',(23.534,-9.37049999999999,16.8));
#215292=CARTESIAN_POINT('Origin',(23.734,-9.8705,14.8));
#215293=CARTESIAN_POINT('',(23.734,-9.8705,14.8));
#215294=CARTESIAN_POINT('',(23.734,-9.92234999999999,14.6963));
#215295=CARTESIAN_POINT('',(23.534,-9.8705,14.8));
#215296=CARTESIAN_POINT('',(23.734,-9.8705,14.8));
#215297=CARTESIAN_POINT('',(23.534,-8.87049999999999,16.8));
#215298=CARTESIAN_POINT('Origin',(23.734,-10.8705,16.8));
#215299=CARTESIAN_POINT('',(23.734,-10.8705,16.8));
#215300=CARTESIAN_POINT('',(23.734,-4.50234999999999,4.0637));
#215301=CARTESIAN_POINT('',(23.534,-10.8705,16.8));
#215302=CARTESIAN_POINT('',(23.734,-10.8705,16.8));
#215303=CARTESIAN_POINT('',(23.534,-10.8705,16.8));
#215304=CARTESIAN_POINT('Origin',(23.734,-10.3705,16.8));
#215305=CARTESIAN_POINT('',(23.734,-10.3705,16.8));
#215306=CARTESIAN_POINT('',(23.734,4.42025,16.8));
#215307=CARTESIAN_POINT('',(23.534,-10.3705,16.8));
#215308=CARTESIAN_POINT('',(23.734,-10.3705,16.8));
#215309=CARTESIAN_POINT('',(23.534,-10.3705,16.8));
#215310=CARTESIAN_POINT('Origin',(23.734,-10.3705,19.2));
#215311=CARTESIAN_POINT('',(23.734,-10.3705,19.2));
#215312=CARTESIAN_POINT('',(23.734,-10.3705,9.6));
#215313=CARTESIAN_POINT('',(23.534,-10.3705,19.2));
#215314=CARTESIAN_POINT('',(23.734,-10.3705,19.2));
#215315=CARTESIAN_POINT('',(23.534,-10.3705,19.2));
#215316=CARTESIAN_POINT('Origin',(23.734,-9.37049999999999,19.2));
#215317=CARTESIAN_POINT('',(23.734,4.92025,19.2));
#215318=CARTESIAN_POINT('',(23.534,-9.37049999999999,19.2));
#215319=CARTESIAN_POINT('Origin',(23.734,-9.8705,17.));
#215320=CARTESIAN_POINT('',(23.734,-9.8705,20.));
#215321=CARTESIAN_POINT('Origin',(23.734,-9.8705,17.));
#215322=CARTESIAN_POINT('',(23.534,-9.8705,20.));
#215323=CARTESIAN_POINT('',(23.734,-9.8705,20.));
#215324=CARTESIAN_POINT('Origin',(23.534,-9.8705,17.));
#215325=CARTESIAN_POINT('Origin',(23.534,-9.8705,17.));
#215326=CARTESIAN_POINT('Origin',(23.734,19.211,0.));
#215327=CARTESIAN_POINT('Origin',(23.734,19.211,0.));
#215328=CARTESIAN_POINT('Origin',(23.734,0.129500000000004,17.));
#215329=CARTESIAN_POINT('',(17.734,0.129500000000003,21.));
#215330=CARTESIAN_POINT('',(23.734,0.129500000000005,21.));
#215331=CARTESIAN_POINT('Origin',(17.734,0.129500000000004,17.));
#215332=CARTESIAN_POINT('Origin',(17.734,0.129500000000004,17.));
#215333=CARTESIAN_POINT('Origin',(17.734,10.1295,7.));
#215334=CARTESIAN_POINT('Origin',(23.734,-9.8705,7.));
#215335=CARTESIAN_POINT('',(17.734,-9.8705,12.));
#215336=CARTESIAN_POINT('',(23.734,-9.8705,12.));
#215337=CARTESIAN_POINT('Origin',(17.734,-9.8705,7.));
#215338=CARTESIAN_POINT('Origin',(17.734,-9.8705,7.));
#215339=CARTESIAN_POINT('Origin',(-23.734,-9.8705,7.));
#215340=CARTESIAN_POINT('',(-23.734,-3.8705,7.));
#215341=CARTESIAN_POINT('',(-23.734,-5.8705,11.4721359549996));
#215342=CARTESIAN_POINT('Origin',(-23.734,-9.8705,7.));
#215343=CARTESIAN_POINT('',(-23.534,-5.8705,11.4721359549996));
#215344=CARTESIAN_POINT('',(-23.734,-5.8705,11.4721359549996));
#215345=CARTESIAN_POINT('',(-23.534,-3.87049999999999,7.));
#215346=CARTESIAN_POINT('Origin',(-23.534,-9.8705,7.));
#215347=CARTESIAN_POINT('',(-23.734,-3.8705,7.));
#215348=CARTESIAN_POINT('Origin',(-23.734,4.1295,7.));
#215349=CARTESIAN_POINT('',(-23.734,4.1295,7.));
#215350=CARTESIAN_POINT('',(-23.734,-7.41125,7.));
#215351=CARTESIAN_POINT('',(-23.534,4.1295,7.));
#215352=CARTESIAN_POINT('',(-23.534,4.1295,7.));
#215353=CARTESIAN_POINT('',(-23.734,4.1295,7.));
#215354=CARTESIAN_POINT('Origin',(-23.734,10.1295,7.));
#215355=CARTESIAN_POINT('',(-23.734,6.1295,11.4721359549996));
#215356=CARTESIAN_POINT('Origin',(-23.734,10.1295,7.));
#215357=CARTESIAN_POINT('',(-23.534,6.1295,11.4721359549996));
#215358=CARTESIAN_POINT('Origin',(-23.534,10.1295,7.));
#215359=CARTESIAN_POINT('',(-23.734,6.1295,11.4721359549996));
#215360=CARTESIAN_POINT('Origin',(-23.734,6.1295,22.));
#215361=CARTESIAN_POINT('',(-23.734,6.1295,11.));
#215362=CARTESIAN_POINT('',(-23.534,6.1295,22.));
#215363=CARTESIAN_POINT('Origin',(-23.734,-5.8705,11.4721359549996));
#215364=CARTESIAN_POINT('',(-23.734,-5.8705,5.73606797749979));
#215365=CARTESIAN_POINT('',(-23.534,-5.8705,22.));
#215366=CARTESIAN_POINT('Origin',(-23.534,0.129500000000005,11.5));
#215367=CARTESIAN_POINT('',(-23.534,0.129500000000002,21.));
#215368=CARTESIAN_POINT('Origin',(-23.534,0.129500000000004,17.));
#215369=CARTESIAN_POINT('',(-23.534,-9.8705,12.));
#215370=CARTESIAN_POINT('Origin',(-23.534,-9.8705,7.));
#215371=CARTESIAN_POINT('Origin',(-23.734,-9.37049999999999,16.8));
#215372=CARTESIAN_POINT('',(-23.734,-9.37049999999999,16.8));
#215373=CARTESIAN_POINT('',(-23.734,-9.37049999999999,19.2));
#215374=CARTESIAN_POINT('',(-23.734,-9.3705,8.4));
#215375=CARTESIAN_POINT('',(-23.534,-9.37049999999999,19.2));
#215376=CARTESIAN_POINT('',(-23.734,-9.37049999999999,19.2));
#215377=CARTESIAN_POINT('',(-23.534,-9.37049999999999,16.8));
#215378=CARTESIAN_POINT('',(-23.534,-9.37049999999999,19.2));
#215379=CARTESIAN_POINT('',(-23.734,-9.37049999999999,16.8));
#215380=CARTESIAN_POINT('Origin',(-23.734,-8.87049999999999,16.8));
#215381=CARTESIAN_POINT('',(-23.734,-8.87049999999999,16.8));
#215382=CARTESIAN_POINT('',(-23.734,-13.91125,16.8));
#215383=CARTESIAN_POINT('',(-23.534,-8.87049999999999,16.8));
#215384=CARTESIAN_POINT('',(-23.534,-9.37049999999999,16.8));
#215385=CARTESIAN_POINT('',(-23.734,-8.87049999999999,16.8));
#215386=CARTESIAN_POINT('Origin',(-23.734,-9.8705,14.8));
#215387=CARTESIAN_POINT('',(-23.734,-9.8705,14.8));
#215388=CARTESIAN_POINT('',(-23.734,-13.73865,7.0637));
#215389=CARTESIAN_POINT('',(-23.534,-9.8705,14.8));
#215390=CARTESIAN_POINT('',(-23.534,-8.87049999999999,16.8));
#215391=CARTESIAN_POINT('',(-23.734,-9.8705,14.8));
#215392=CARTESIAN_POINT('Origin',(-23.734,-10.8705,16.8));
#215393=CARTESIAN_POINT('',(-23.734,-10.8705,16.8));
#215394=CARTESIAN_POINT('',(-23.734,-8.31864999999999,11.6963));
#215395=CARTESIAN_POINT('',(-23.534,-10.8705,16.8));
#215396=CARTESIAN_POINT('',(-23.534,-10.8705,16.8));
#215397=CARTESIAN_POINT('',(-23.734,-10.8705,16.8));
#215398=CARTESIAN_POINT('Origin',(-23.734,-10.3705,16.8));
#215399=CARTESIAN_POINT('',(-23.734,-10.3705,16.8));
#215400=CARTESIAN_POINT('',(-23.734,-14.66125,16.8));
#215401=CARTESIAN_POINT('',(-23.534,-10.3705,16.8));
#215402=CARTESIAN_POINT('',(-23.534,-10.3705,16.8));
#215403=CARTESIAN_POINT('',(-23.734,-10.3705,16.8));
#215404=CARTESIAN_POINT('Origin',(-23.734,-10.3705,19.2));
#215405=CARTESIAN_POINT('',(-23.734,-10.3705,19.2));
#215406=CARTESIAN_POINT('',(-23.734,-10.3705,9.6));
#215407=CARTESIAN_POINT('',(-23.534,-10.3705,19.2));
#215408=CARTESIAN_POINT('',(-23.534,-10.3705,19.2));
#215409=CARTESIAN_POINT('',(-23.734,-10.3705,19.2));
#215410=CARTESIAN_POINT('Origin',(-23.734,-9.37049999999999,19.2));
#215411=CARTESIAN_POINT('',(-23.734,-14.16125,19.2));
#215412=CARTESIAN_POINT('',(-23.534,-9.37049999999999,19.2));
#215413=CARTESIAN_POINT('Origin',(-23.734,-9.8705,17.));
#215414=CARTESIAN_POINT('',(-23.534,-9.8705,20.));
#215415=CARTESIAN_POINT('Origin',(-23.534,-9.8705,17.));
#215416=CARTESIAN_POINT('',(-23.734,-9.8705,20.));
#215417=CARTESIAN_POINT('',(-23.734,-9.8705,20.));
#215418=CARTESIAN_POINT('Origin',(-23.734,-9.8705,17.));
#215419=CARTESIAN_POINT('Origin',(-23.534,-9.8705,17.));
#215420=CARTESIAN_POINT('Origin',(-23.734,9.62950000000001,14.8));
#215421=CARTESIAN_POINT('',(-23.734,9.62950000000001,14.8));
#215422=CARTESIAN_POINT('',(-23.734,10.6295,14.8));
#215423=CARTESIAN_POINT('',(-23.734,-4.66124999999999,14.8));
#215424=CARTESIAN_POINT('',(-23.534,10.6295,14.8));
#215425=CARTESIAN_POINT('',(-23.734,10.6295,14.8));
#215426=CARTESIAN_POINT('',(-23.534,9.62950000000001,14.8));
#215427=CARTESIAN_POINT('',(-23.534,10.6295,14.8));
#215428=CARTESIAN_POINT('',(-23.734,9.62950000000001,14.8));
#215429=CARTESIAN_POINT('Origin',(-23.734,9.62950000000001,17.2));
#215430=CARTESIAN_POINT('',(-23.734,9.62950000000001,17.2));
#215431=CARTESIAN_POINT('',(-23.734,9.62950000000001,8.6));
#215432=CARTESIAN_POINT('',(-23.534,9.62950000000001,17.2));
#215433=CARTESIAN_POINT('',(-23.534,9.62950000000001,14.8));
#215434=CARTESIAN_POINT('',(-23.734,9.62950000000001,17.2));
#215435=CARTESIAN_POINT('Origin',(-23.734,9.12950000000001,17.2));
#215436=CARTESIAN_POINT('',(-23.734,9.12950000000001,17.2));
#215437=CARTESIAN_POINT('',(-23.734,-4.91124999999999,17.2));
#215438=CARTESIAN_POINT('',(-23.534,9.12950000000001,17.2));
#215439=CARTESIAN_POINT('',(-23.534,9.62950000000001,17.2));
#215440=CARTESIAN_POINT('',(-23.734,9.12950000000001,17.2));
#215441=CARTESIAN_POINT('Origin',(-23.734,10.1295,19.2));
#215442=CARTESIAN_POINT('',(-23.734,10.1295,19.2));
#215443=CARTESIAN_POINT('',(-23.734,3.38135000000002,5.7037));
#215444=CARTESIAN_POINT('',(-23.534,10.1295,19.2));
#215445=CARTESIAN_POINT('',(-23.534,9.12950000000001,17.2));
#215446=CARTESIAN_POINT('',(-23.734,10.1295,19.2));
#215447=CARTESIAN_POINT('Origin',(-23.734,11.1295,17.2));
#215448=CARTESIAN_POINT('',(-23.734,11.1295,17.2));
#215449=CARTESIAN_POINT('',(-23.734,11.56135,16.3363));
#215450=CARTESIAN_POINT('',(-23.534,11.1295,17.2));
#215451=CARTESIAN_POINT('',(-23.534,11.1295,17.2));
#215452=CARTESIAN_POINT('',(-23.734,11.1295,17.2));
#215453=CARTESIAN_POINT('Origin',(-23.734,10.6295,17.2));
#215454=CARTESIAN_POINT('',(-23.734,10.6295,17.2));
#215455=CARTESIAN_POINT('',(-23.734,-4.16125,17.2));
#215456=CARTESIAN_POINT('',(-23.534,10.6295,17.2));
#215457=CARTESIAN_POINT('',(-23.534,10.6295,17.2));
#215458=CARTESIAN_POINT('',(-23.734,10.6295,17.2));
#215459=CARTESIAN_POINT('Origin',(-23.734,10.6295,14.8));
#215460=CARTESIAN_POINT('',(-23.734,10.6295,7.4));
#215461=CARTESIAN_POINT('',(-23.534,10.6295,14.8));
#215462=CARTESIAN_POINT('Origin',(-23.734,10.1295,17.));
#215463=CARTESIAN_POINT('',(-23.534,10.1295,20.));
#215464=CARTESIAN_POINT('Origin',(-23.534,10.1295,17.));
#215465=CARTESIAN_POINT('',(-23.734,10.1295,20.));
#215466=CARTESIAN_POINT('',(-23.734,10.1295,20.));
#215467=CARTESIAN_POINT('Origin',(-23.734,10.1295,17.));
#215468=CARTESIAN_POINT('Origin',(-23.534,10.1295,17.));
#215469=CARTESIAN_POINT('Origin',(-23.734,-18.952,0.));
#215470=CARTESIAN_POINT('Origin',(-23.734,-18.952,0.));
#215471=CARTESIAN_POINT('Origin',(-23.734,-18.952,0.));
#215472=CARTESIAN_POINT('',(-23.734,19.211,0.));
#215473=CARTESIAN_POINT('',(-23.734,19.211,0.));
#215474=CARTESIAN_POINT('',(-23.734,-18.952,0.));
#215475=CARTESIAN_POINT('',(-23.734,19.211,0.));
#215476=CARTESIAN_POINT('',(-23.734,-18.952,0.));
#215477=CARTESIAN_POINT('Origin',(-17.734,10.1295,7.));
#215478=CARTESIAN_POINT('Origin',(-23.734,-9.8705,7.));
#215479=CARTESIAN_POINT('',(-17.734,-9.8705,12.));
#215480=CARTESIAN_POINT('Origin',(-17.734,-9.8705,7.));
#215481=CARTESIAN_POINT('',(-23.734,-9.8705,12.));
#215482=CARTESIAN_POINT('Origin',(-17.734,-9.8705,7.));
#215483=CARTESIAN_POINT('Origin',(-23.734,0.129500000000004,17.));
#215484=CARTESIAN_POINT('',(-17.734,0.129500000000003,21.));
#215485=CARTESIAN_POINT('Origin',(-17.734,0.129500000000004,17.));
#215486=CARTESIAN_POINT('',(-23.734,0.129500000000005,21.));
#215487=CARTESIAN_POINT('Origin',(-17.734,0.129500000000004,17.));
#215488=CARTESIAN_POINT('Origin',(-18.734,0.12950000000008,22.));
#215489=CARTESIAN_POINT('',(-21.234,0.12950000000008,21.5));
#215490=CARTESIAN_POINT('Origin',(-18.734,0.12950000000008,21.5));
#215491=CARTESIAN_POINT('',(-21.234,0.12950000000008,22.));
#215492=CARTESIAN_POINT('Origin',(0.,0.12950000000008,21.5));
#215493=CARTESIAN_POINT('Origin',(18.734,0.12950000000008,22.));
#215494=CARTESIAN_POINT('',(16.234,0.12950000000008,21.5));
#215495=CARTESIAN_POINT('Origin',(18.734,0.12950000000008,21.5));
#215496=CARTESIAN_POINT('',(16.234,0.12950000000008,22.));
#215497=CARTESIAN_POINT('Origin',(0.,0.12950000000008,21.5));
#215498=CARTESIAN_POINT('Origin',(-7.0995,19.4175,0.));
#215499=CARTESIAN_POINT('',(-7.0995,19.4175,0.));
#215500=CARTESIAN_POINT('',(-7.0995,16.8045,0.));
#215501=CARTESIAN_POINT('',(-7.0995,19.4175,0.));
#215502=CARTESIAN_POINT('Origin',(-10.7505,17.8045,0.));
#215503=CARTESIAN_POINT('Origin',(-10.7505,17.8045,0.));
#215504=CARTESIAN_POINT('Origin',(-9.06658668237251,24.2952266006623,0.));
#215505=CARTESIAN_POINT('',(-9.06658668237251,24.4862266006622,0.));
#215506=CARTESIAN_POINT('Origin',(-9.06658668237251,24.2952266006623,0.));
#215507=CARTESIAN_POINT('',(-9.06658668237251,24.4862266006622,0.));
#215508=CARTESIAN_POINT('Origin',(-7.30158668237251,24.4862266006622,0.));
#215509=CARTESIAN_POINT('',(-7.30158668237251,24.4862266006622,0.));
#215510=CARTESIAN_POINT('',(-9.06658668237251,24.4862266006622,0.));
#215511=CARTESIAN_POINT('',(-7.30158668237251,24.4862266006622,0.));
#215512=CARTESIAN_POINT('Origin',(-7.30158668237251,24.6772266006623,0.));
#215513=CARTESIAN_POINT('',(-7.11058668237251,24.6772266006623,0.));
#215514=CARTESIAN_POINT('Origin',(-7.30158668237251,24.6772266006623,0.));
#215515=CARTESIAN_POINT('',(-7.11058668237251,24.6772266006623,0.));
#215516=CARTESIAN_POINT('Origin',(-7.11058668237251,25.8032266006623,0.));
#215517=CARTESIAN_POINT('',(-7.11058668237251,25.8032266006623,0.));
#215518=CARTESIAN_POINT('',(-7.11058668237251,24.6772266006623,0.));
#215519=CARTESIAN_POINT('',(-7.11058668237251,25.8032266006623,0.));
#215520=CARTESIAN_POINT('Origin',(-7.36458668237251,25.8032266006623,0.));
#215521=CARTESIAN_POINT('',(-7.36458668237251,26.0572266006623,0.));
#215522=CARTESIAN_POINT('Origin',(-7.36458668237251,25.8032266006623,0.));
#215523=CARTESIAN_POINT('',(-7.36458668237251,26.0572266006623,0.));
#215524=CARTESIAN_POINT('Origin',(-18.734,24.211,0.));
#215525=CARTESIAN_POINT('',(-18.734,24.211,0.));
#215526=CARTESIAN_POINT('',(-7.36458668237251,26.0572266006622,0.));
#215527=CARTESIAN_POINT('',(-18.734,24.211,0.));
#215528=CARTESIAN_POINT('Origin',(-18.734,19.211,0.));
#215529=CARTESIAN_POINT('Origin',(-18.734,19.211,0.));
#215530=CARTESIAN_POINT('Origin',(-18.734,-18.952,0.));
#215531=CARTESIAN_POINT('',(-18.734,-23.952,0.));
#215532=CARTESIAN_POINT('Origin',(-18.734,-18.952,0.));
#215533=CARTESIAN_POINT('',(-18.734,-23.952,0.));
#215534=CARTESIAN_POINT('Origin',(18.734,-23.952,0.));
#215535=CARTESIAN_POINT('',(18.734,-23.952,0.));
#215536=CARTESIAN_POINT('',(-18.734,-23.952,0.));
#215537=CARTESIAN_POINT('',(18.734,-23.952,0.));
#215538=CARTESIAN_POINT('Origin',(18.734,-18.952,0.));
#215539=CARTESIAN_POINT('',(23.734,-18.952,0.));
#215540=CARTESIAN_POINT('Origin',(18.734,-18.952,0.));
#215541=CARTESIAN_POINT('',(23.734,-18.952,0.));
#215542=CARTESIAN_POINT('Origin',(23.734,19.211,0.));
#215543=CARTESIAN_POINT('',(23.734,19.211,0.));
#215544=CARTESIAN_POINT('',(23.734,19.211,0.));
#215545=CARTESIAN_POINT('',(23.734,19.211,0.));
#215546=CARTESIAN_POINT('Origin',(18.734,19.211,0.));
#215547=CARTESIAN_POINT('',(18.734,24.211,0.));
#215548=CARTESIAN_POINT('Origin',(18.734,19.211,0.));
#215549=CARTESIAN_POINT('',(18.734,24.211,0.));
#215550=CARTESIAN_POINT('Origin',(7.36458668237251,26.0572266006622,0.));
#215551=CARTESIAN_POINT('',(7.36458668237251,26.0572266006622,0.));
#215552=CARTESIAN_POINT('',(7.36458668237251,26.0572266006622,0.));
#215553=CARTESIAN_POINT('',(7.36458668237251,26.0572266006622,0.));
#215554=CARTESIAN_POINT('Origin',(7.36458668237251,25.8032266006622,0.));
#215555=CARTESIAN_POINT('',(7.11058668237251,25.8032266006622,0.));
#215556=CARTESIAN_POINT('Origin',(7.36458668237251,25.8032266006622,0.));
#215557=CARTESIAN_POINT('',(7.11058668237251,25.8032266006622,0.));
#215558=CARTESIAN_POINT('Origin',(7.11058668237251,24.6772266006623,0.));
#215559=CARTESIAN_POINT('',(7.11058668237251,24.6772266006623,0.));
#215560=CARTESIAN_POINT('',(7.11058668237251,24.6772266006623,0.));
#215561=CARTESIAN_POINT('',(7.11058668237251,24.6772266006623,0.));
#215562=CARTESIAN_POINT('Origin',(7.30158668237251,24.6772266006623,0.));
#215563=CARTESIAN_POINT('',(7.30158668237251,24.4862266006622,0.));
#215564=CARTESIAN_POINT('Origin',(7.30158668237251,24.6772266006623,0.));
#215565=CARTESIAN_POINT('',(7.30158668237251,24.4862266006622,0.));
#215566=CARTESIAN_POINT('Origin',(9.06658668237251,24.4862266006622,0.));
#215567=CARTESIAN_POINT('',(9.06658668237251,24.4862266006622,0.));
#215568=CARTESIAN_POINT('',(9.06658668237251,24.4862266006622,0.));
#215569=CARTESIAN_POINT('',(9.06658668237251,24.4862266006622,0.));
#215570=CARTESIAN_POINT('Origin',(9.06658668237251,24.2952266006623,0.));
#215571=CARTESIAN_POINT('',(9.25758668237251,24.2952266006623,0.));
#215572=CARTESIAN_POINT('Origin',(9.06658668237251,24.2952266006623,0.));
#215573=CARTESIAN_POINT('',(9.25758668237251,24.2952266006623,0.));
#215574=CARTESIAN_POINT('Origin',(9.25758668237251,21.5062266006623,0.));
#215575=CARTESIAN_POINT('',(9.25758668237251,21.5062266006623,0.));
#215576=CARTESIAN_POINT('',(9.25758668237251,21.5062266006623,0.));
#215577=CARTESIAN_POINT('',(9.25758668237251,21.5062266006623,0.));
#215578=CARTESIAN_POINT('Origin',(10.7505,17.8045,0.));
#215579=CARTESIAN_POINT('Origin',(10.7505,17.8045,0.));
#215580=CARTESIAN_POINT('Origin',(0.,1.05261330033112,0.));
#215597=UNCERTAINTY_MEASURE_WITH_UNIT(LENGTH_MEASURE(0.01),#215610,
'DISTANCE_ACCURACY_VALUE',
'Maximum model space distance between geometric entities at asserted c
onnectivities');
#215598=UNCERTAINTY_MEASURE_WITH_UNIT(LENGTH_MEASURE(0.01),#215610,
'DISTANCE_ACCURACY_VALUE',
'Maximum model space distance between geometric entities at asserted c
onnectivities');
#215608=(
GEOMETRIC_REPRESENTATION_CONTEXT(3)
GLOBAL_UNCERTAINTY_ASSIGNED_CONTEXT((#215597))
GLOBAL_UNIT_ASSIGNED_CONTEXT((#215610,#215612,#215613))
REPRESENTATION_CONTEXT('','3D')
);
#215609=(
GEOMETRIC_REPRESENTATION_CONTEXT(3)
GLOBAL_UNCERTAINTY_ASSIGNED_CONTEXT((#215598))
GLOBAL_UNIT_ASSIGNED_CONTEXT((#215610,#215612,#215613))
REPRESENTATION_CONTEXT('','3D')
);
#215610=(
LENGTH_UNIT()
NAMED_UNIT(*)
SI_UNIT(.MILLI.,.METRE.)
);
#215612=(
NAMED_UNIT(*)
PLANE_ANGLE_UNIT()
SI_UNIT($,.RADIAN.)
);
#215613=(
NAMED_UNIT(*)
SI_UNIT($,.STERADIAN.)
SOLID_ANGLE_UNIT()
);
#215623=SHAPE_DEFINITION_REPRESENTATION(#215635,#215652);
#215635=PRODUCT_DEFINITION_SHAPE('',$,#215663);
#215652=SHAPE_REPRESENTATION('',(#29720),#215608);
#215653=PRODUCT_DEFINITION_CONTEXT('part definition',#215685,'design');
#215663=PRODUCT_DEFINITION('2026-10-04-13-44-26-617_1',
'End_Cap(Mirror)',#215673,#215653);
#215673=PRODUCT_DEFINITION_FORMATION('',$,#215696);
#215685=APPLICATION_CONTEXT(
'Core Data for Automotive Mechanical Design Process');
#215686=PRODUCT_CONTEXT('part definition',#215685,'mechanical');
#215696=PRODUCT('2026-10-04-13-44-26-617_1','End_Cap(Mirror)',$,(#215686));
#215698=PRESENTATION_STYLE_ASSIGNMENT((#215700));
#215700=SURFACE_STYLE_USAGE(.BOTH.,#215702);
#215702=SURFACE_SIDE_STYLE('',(#215704));
#215704=SURFACE_STYLE_FILL_AREA(#215706);
#215706=FILL_AREA_STYLE('Opaque(245,245,246)',(#215708));
#215708=FILL_AREA_STYLE_COLOUR('Opaque(245,245,246)',#215710);
#215710=COLOUR_RGB('Opaque(245,245,246)', 0.66274510, 0.83137255, 0.94901961);
ENDSEC;
END-ISO-10303-21;
